ISO-10303-21;
HEADER;
FILE_DESCRIPTION (('STEP AP214'),
    '1' );
FILE_NAME ('1.3 Jaw Plate.step',
    '2026-10-06T08:51:13',
    ( '' ),
    ( '' ),
    'SwSTEP 2.0',
    'SolidWorks 2021',
    '' );
FILE_SCHEMA (( 'AUTOMOTIVE_DESIGN' ));
ENDSEC;

DATA;
#3=ADVANCED_FACE ( 'NONE', ( #5101 ), #71138, .F. ) ;
#5=VECTOR ( 'NONE', #78980, 1000.000000000000227 ) ;
#7=ORIENTED_EDGE ( 'NONE', *, *, #104399, .F. ) ;
#8=EDGE_LOOP ( 'NONE', ( #83544, #1856, #131189, #37000 ) ) ;
#9=FACE_OUTER_BOUND ( 'NONE', #81012, .T. ) ;
#10=VECTOR ( 'NONE', #93764, 1000.000000000000000 ) ;
#11=AXIS2_PLACEMENT_3D ( 'NONE', #21199, #109633, #54568 ) ;
#12=VECTOR ( 'NONE', #112321, 1000.000000000000000 ) ;
#13=( BOUNDED_CURVE ( )  B_SPLINE_CURVE ( 3, ( #128504, #27742, #103166, #38633 ),
 .UNSPECIFIED., .F., .T. ) 
 B_SPLINE_CURVE_WITH_KNOTS ( ( 4, 4 ),
 ( 5.143245962375963209, 6.645403452391246191 ),
 .UNSPECIFIED. ) 
 CURVE ( )  GEOMETRIC_REPRESENTATION_ITEM ( )  RATIONAL_B_SPLINE_CURVE ( ( 1.000000000000000000, 0.8206354192515237234, 0.8206354192515237234, 1.000000000000000000 ) ) 
 REPRESENTATION_ITEM ( '' )  );
#15=ORIENTED_EDGE ( 'NONE', *, *, #47014, .F. ) ;
#16=VERTEX_POINT ( 'NONE', #58144 ) ;
#18=ORIENTED_EDGE ( 'NONE', *, *, #122540, .F. ) ;
#19=CARTESIAN_POINT ( 'NONE',  ( -20.20710678118640402, -14.24070752338413826, 5.000000000000000000 ) ) ;
#24=ORIENTED_EDGE ( 'NONE', *, *, #19090, .F. ) ;
#25=LINE ( 'NONE', #44323, #82672 ) ;
#26=ORIENTED_EDGE ( 'NONE', *, *, #3909, .F. ) ;
#29=ORIENTED_EDGE ( 'NONE', *, *, #119403, .F. ) ;
#30=VECTOR ( 'NONE', #87246, 1000.000000000000000 ) ;
#31=VECTOR ( 'NONE', #125646, 1000.000000000000227 ) ;
#32=PLANE ( 'NONE',  #68433 ) ;
#35=FACE_OUTER_BOUND ( 'NONE', #136835, .T. ) ;
#36=LINE ( 'NONE', #90690, #18133 ) ;
#37=PLANE ( 'NONE',  #65195 ) ;
#38=ADVANCED_FACE ( 'NONE', ( #115284 ), #3675, .F. ) ;
#39=FACE_BOUND ( 'NONE', #50173, .T. ) ;
#40=ORIENTED_EDGE ( 'NONE', *, *, #20313, .F. ) ;
#41=CARTESIAN_POINT ( 'NONE',  ( -29.99451991528749417, 28.92564299267958816, 4.000000000000000000 ) ) ;
#42=EDGE_CURVE ( 'NONE', #25059, #21205, #27594, .T. ) ;
#43=EDGE_CURVE ( 'NONE', #65963, #18880, #92855, .T. ) ;
#45=DIRECTION ( 'NONE',  ( 0.3543493200069162685, -0.000000000000000000, -0.9351131265310288487 ) ) ;
#46=DIRECTION ( 'NONE',  ( 1.000000000000000000, 0.000000000000000000, -0.000000000000000000 ) ) ;
#47=ORIENTED_EDGE ( 'NONE', *, *, #35015, .F. ) ;
#48=LINE ( 'NONE', #77678, #78225 ) ;
#49=EDGE_LOOP ( 'NONE', ( #96646, #108093, #78224, #23588 ) ) ;
#51=LINE ( 'NONE', #32014, #142062 ) ;
#53=EDGE_CURVE ( 'NONE', #25081, #19559, #82032, .T. ) ;
#54=EDGE_CURVE ( 'NONE', #25745, #125467, #104441, .T. ) ;
#58=DIRECTION ( 'NONE',  ( -0.7071067811865486830, -0.7071067811865464625, 0.000000000000000000 ) ) ;
#60=ADVANCED_FACE ( 'NONE', ( #80585 ), #50094, .F. ) ;
#61=CARTESIAN_POINT ( 'NONE',  ( 68.99451991528748351, 28.92564299267986172, 4.000000000000000000 ) ) ;
#62=EDGE_LOOP ( 'NONE', ( #94258, #115607, #50312, #53192 ) ) ;
#63=AXIS2_PLACEMENT_3D ( 'NONE', #104309, #85415, #117326 ) ;
#64=CARTESIAN_POINT ( 'NONE',  ( 34.92499999999998295, -21.72500000000000142, 5.000000000000000000 ) ) ;
#65=EDGE_CURVE ( 'NONE', #58716, #118828, #49403, .T. ) ;
#67=DIRECTION ( 'NONE',  ( -0.7071067811865486830, -0.7071067811865464625, 0.000000000000000000 ) ) ;
#69=LINE ( 'NONE', #66808, #128074 ) ;
#70=DIRECTION ( 'NONE',  ( -0.7071067811865486830, -0.7071067811865464625, 0.000000000000000000 ) ) ;
#71=ORIENTED_EDGE ( 'NONE', *, *, #64035, .T. ) ;
#72=ORIENTED_EDGE ( 'NONE', *, *, #68229, .T. ) ;
#74=EDGE_LOOP ( 'NONE', ( #63334, #111913, #607, #124092 ) ) ;
#75=FACE_OUTER_BOUND ( 'NONE', #77019, .T. ) ;
#76=EDGE_CURVE ( 'NONE', #54574, #78177, #14595, .T. ) ;
#77=DIRECTION ( 'NONE',  ( 0.3543493200069162685, -0.000000000000000000, -0.9351131265310288487 ) ) ;
#78=ORIENTED_EDGE ( 'NONE', *, *, #62615, .T. ) ;
#79=ORIENTED_EDGE ( 'NONE', *, *, #43969, .T. ) ;
#81=DIRECTION ( 'NONE',  ( 1.000000000000000000, 0.000000000000000000, 0.000000000000000000 ) ) ;
#82=CARTESIAN_POINT ( 'NONE',  ( 0.000000000000000000, 0.000000000000000000, 5.000000000000000000 ) ) ;
#83=ORIENTED_EDGE ( 'NONE', *, *, #34651, .F. ) ;
#84=DIRECTION ( 'NONE',  ( 0.3543493200069162685, -0.000000000000000000, -0.9351131265310288487 ) ) ;
#85=EDGE_CURVE ( 'NONE', #114150, #6491, #116025, .T. ) ;
#86=VECTOR ( 'NONE', #59606, 1000.000000000000000 ) ;
#87=CARTESIAN_POINT ( 'NONE',  ( -9.489213562373095101, -27.52281430457062328, 5.000000000000000000 ) ) ;
#89=CARTESIAN_POINT ( 'NONE',  ( 14.99999999999989519, -2.904428200921294057, -6.989807076074975534 ) ) ;
#90=ORIENTED_EDGE ( 'NONE', *, *, #118546, .F. ) ;
#92=CARTESIAN_POINT ( 'NONE',  ( -19.83905809817562016, 22.22500000000000142, 10.71662732872346169 ) ) ;
#93=EDGE_CURVE ( 'NONE', #95062, #84583, #91456, .T. ) ;
#94=DIRECTION ( 'NONE',  ( -0.6830127018922180770, -0.6830127018922204085, -0.2588190451025213501 ) ) ;
#95=CARTESIAN_POINT ( 'NONE',  ( 20.99999999999985079, 12.25461709320622639, -10.07315571508692464 ) ) ;
#96=ORIENTED_EDGE ( 'NONE', *, *, #90476, .F. ) ;
#97=DIRECTION ( 'NONE',  ( -0.000000000000000000, 0.000000000000000000, 1.000000000000000000 ) ) ;
#98=ORIENTED_EDGE ( 'NONE', *, *, #70389, .T. ) ;
#99=DIRECTION ( 'NONE',  ( -0.7071067811865486830, 0.7071067811865464625, 0.000000000000000000 ) ) ;
#100=VECTOR ( 'NONE', #124280, 1000.000000000000000 ) ;
#101=CARTESIAN_POINT ( 'NONE',  ( 3.489213562373097322, -27.52281430457057709, 5.000000000000000000 ) ) ;
#103=ORIENTED_EDGE ( 'NONE', *, *, #12795, .T. ) ;
#104=ADVANCED_FACE ( 'NONE', ( #137820 ), #15976, .T. ) ;
#105=VECTOR ( 'NONE', #70002, 1000.000000000000227 ) ;
#106=EDGE_CURVE ( 'NONE', #132598, #105272, #69721, .T. ) ;
#109=ORIENTED_EDGE ( 'NONE', *, *, #66738, .T. ) ;
#110=AXIS2_PLACEMENT_3D ( 'NONE', #91463, #135678, #48666 ) ;
#111=VECTOR ( 'NONE', #117132, 999.9999999999998863 ) ;
#113=DIRECTION ( 'NONE',  ( -0.7071067811865487940, 0.7071067811865463515, -0.000000000000000000 ) ) ;
#114=VECTOR ( 'NONE', #50874, 1000.000000000000000 ) ;
#115=LINE ( 'NONE', #86474, #33098 ) ;
#116=EDGE_CURVE ( 'NONE', #31169, #8752, #138521, .T. ) ;
#117=VECTOR ( 'NONE', #30072, 1000.000000000000000 ) ;
#118=EDGE_LOOP ( 'NONE', ( #114372, #70505, #8992, #113022 ) ) ;
#119=LINE ( 'NONE', #77741, #60053 ) ;
#120=DIRECTION ( 'NONE',  ( 0.6830127018922180770, -0.6830127018922204085, -0.2588190451025213501 ) ) ;
#121=VERTEX_POINT ( 'NONE', #68996 ) ;
#122=ORIENTED_EDGE ( 'NONE', *, *, #95989, .T. ) ;
#123=CARTESIAN_POINT ( 'NONE',  ( -13.10742158956126424, 3.736470153597435395, 4.109745541549492565 ) ) ;
#124=AXIS2_PLACEMENT_3D ( 'NONE', #74766, #9441, #75464 ) ;
#125=ORIENTED_EDGE ( 'NONE', *, *, #121353, .T. ) ;
#126=CARTESIAN_POINT ( 'NONE',  ( 25.49999999999982592, -19.53360074219753884, 5.000000000000000000 ) ) ;
#127=DIRECTION ( 'NONE',  ( -0.7071067811865486830, -0.7071067811865464625, 0.000000000000000000 ) ) ;
#128=DIRECTION ( 'NONE',  ( -0.7071067811865486830, 0.7071067811865464625, 0.000000000000000000 ) ) ;
#129=ORIENTED_EDGE ( 'NONE', *, *, #131844, .F. ) ;
#130=EDGE_CURVE ( 'NONE', #6161, #1058, #58874, .T. ) ;
#131=LINE ( 'NONE', #142993, #129973 ) ;
#132=LINE ( 'NONE', #67611, #18945 ) ;
#133=LINE ( 'NONE', #13167, #47104 ) ;
#134=AXIS2_PLACEMENT_3D ( 'NONE', #6194, #104832, #5501 ) ;
#135=LINE ( 'NONE', #42284, #50624 ) ;
#137=CARTESIAN_POINT ( 'NONE',  ( 2.999999999999988898, 2.966399257802230682, 5.000000000000000000 ) ) ;
#138=VECTOR ( 'NONE', #55015, 1000.000000000000000 ) ;
#139=ORIENTED_EDGE ( 'NONE', *, *, #36771, .T. ) ;
#144=VECTOR ( 'NONE', #74034, 999.9999999999998863 ) ;
#145=EDGE_LOOP ( 'NONE', ( #119724, #61454, #57894, #85195 ) ) ;
#146=CARTESIAN_POINT ( 'NONE',  ( -5.708222910169487463, -15.74070752338411694, 19.73771281079096340 ) ) ;
#147=DIRECTION ( 'NONE',  ( -0.7071067811865486830, -0.7071067811865464625, 0.000000000000000000 ) ) ;
#148=VECTOR ( 'NONE', #138557, 1000.000000000000000 ) ;
#149=ORIENTED_EDGE ( 'NONE', *, *, #38243, .F. ) ;
#151=FACE_OUTER_BOUND ( 'NONE', #122556, .T. ) ;
#152=CARTESIAN_POINT ( 'NONE',  ( -7.499999999999947597, -4.796895815301026822, -3.611700055028700174 ) ) ;
#153=ADVANCED_FACE ( 'NONE', ( #103035 ), #103710, .F. ) ;
#154=CARTESIAN_POINT ( 'NONE',  ( -12.18398860626900060, 28.73617430169795739, 5.000000000000000000 ) ) ;
#156=AXIS2_PLACEMENT_3D ( 'NONE', #125719, #134450, #3870 ) ;
#157=ORIENTED_EDGE ( 'NONE', *, *, #128606, .T. ) ;
#158=CARTESIAN_POINT ( 'NONE',  ( 5.207106781186502609, -17.24070752338410983, 5.000000000000000000 ) ) ;
#159=DIRECTION ( 'NONE',  ( 0.7071067811865487940, -0.7071067811865463515, 0.000000000000000000 ) ) ;
#160=FACE_OUTER_BOUND ( 'NONE', #79460, .T. ) ;
#162=PLANE ( 'NONE',  #130794 ) ;
#163=CARTESIAN_POINT ( 'NONE',  ( 19.49999999999985789, 8.319652575858395238, -8.582050562765779489 ) ) ;
#164=FACE_OUTER_BOUND ( 'NONE', #130185, .T. ) ;
#166=DIRECTION ( 'NONE',  ( 0.6830127018922181881, 0.6830127018922202975, -0.2588190451025214056 ) ) ;
#167=EDGE_CURVE ( 'NONE', #60255, #130315, #34540, .T. ) ;
#168=DIRECTION ( 'NONE',  ( 0.7071067811865486830, -0.7071067811865464625, -0.000000000000000000 ) ) ;
#171=ORIENTED_EDGE ( 'NONE', *, *, #96108, .T. ) ;
#173=DIRECTION ( 'NONE',  ( -0.7071067811865486830, -0.7071067811865464625, 0.000000000000000000 ) ) ;
#174=CARTESIAN_POINT ( 'NONE',  ( 53.99451991528749062, 28.92564299267975869, 4.000000000000000000 ) ) ;
#176=DIRECTION ( 'NONE',  ( 0.7071067811865487940, 0.7071067811865463515, 0.000000000000000000 ) ) ;
#178=LINE ( 'NONE', #43032, #32998 ) ;
#179=EDGE_CURVE ( 'NONE', #63680, #108628, #141365, .T. ) ;
#181=ORIENTED_EDGE ( 'NONE', *, *, #134281, .T. ) ;
#183=ORIENTED_EDGE ( 'NONE', *, *, #91628, .T. ) ;
#184=ORIENTED_EDGE ( 'NONE', *, *, #140711, .F. ) ;
#185=VECTOR ( 'NONE', #101958, 1000.000000000000227 ) ;
#187=DIRECTION ( 'NONE',  ( 0.6830127018922181881, 0.6830127018922202975, -0.2588190451025214056 ) ) ;
#188=CARTESIAN_POINT ( 'NONE',  ( -12.29974487139158512, -27.71228299555214747, 4.000000000000000000 ) ) ;
#189=PLANE ( 'NONE',  #18575 ) ;
#190=EDGE_LOOP ( 'NONE', ( #15272, #100026, #80901, #142923 ) ) ;
#191=EDGE_CURVE ( 'NONE', #72974, #90074, #61695, .T. ) ;
#192=DIRECTION ( 'NONE',  ( -0.7071067811865487940, 0.7071067811865463515, 0.000000000000000000 ) ) ;
#193=ORIENTED_EDGE ( 'NONE', *, *, #9062, .T. ) ;
#197=CARTESIAN_POINT ( 'NONE',  ( -34.92500000000001137, 6.856123077392376253, 4.000000000000000000 ) ) ;
#198=PLANE ( 'NONE',  #64849 ) ;
#199=VECTOR ( 'NONE', #98975, 1000.000000000000000 ) ;
#200=DIRECTION ( 'NONE',  ( 1.000000000000000000, 0.000000000000000000, 0.000000000000000000 ) ) ;
#202=DIRECTION ( 'NONE',  ( -0.7071067811865486830, -0.7071067811865464625, -0.000000000000000000 ) ) ;
#205=DIRECTION ( 'NONE',  ( 0.7071067811865486830, -0.7071067811865464625, -0.000000000000000000 ) ) ;
#206=DIRECTION ( 'NONE',  ( -0.000000000000000000, -0.000000000000000000, 1.000000000000000000 ) ) ;
#208=EDGE_LOOP ( 'NONE', ( #82343, #5888, #63190, #69675 ) ) ;
#209=FACE_OUTER_BOUND ( 'NONE', #9634, .T. ) ;
#211=ORIENTED_EDGE ( 'NONE', *, *, #117503, .T. ) ;
#212=VECTOR ( 'NONE', #88205, 1000.000000000000000 ) ;
#214=CARTESIAN_POINT ( 'NONE',  ( 0.000000000000000000, 0.000000000000000000, 5.000000000000000000 ) ) ;
#215=ORIENTED_EDGE ( 'NONE', *, *, #26545, .F. ) ;
#216=CARTESIAN_POINT ( 'NONE',  ( 12.48921356237309155, -27.52281430457064104, 5.000000000000000000 ) ) ;
#217=CARTESIAN_POINT ( 'NONE',  ( 29.99999999999979039, -10.77435723561692704, -9.972017380717296930 ) ) ;
#218=VECTOR ( 'NONE', #139975, 1000.000000000000000 ) ;
#219=VECTOR ( 'NONE', #138745, 1000.000000000000000 ) ;
#220=AXIS2_PLACEMENT_3D ( 'NONE', #21758, #55108, #75432 ) ;
#222=EDGE_CURVE ( 'NONE', #139983, #86102, #20281, .T. ) ;
#223=AXIS2_PLACEMENT_3D ( 'NONE', #89988, #15261, #133521 ) ;
#224=FACE_OUTER_BOUND ( 'NONE', #124706, .T. ) ;
#225=FACE_BOUND ( 'NONE', #102384, .T. ) ;
#226=ADVANCED_FACE ( 'NONE', ( #51523 ), #94983, .F. ) ;
#227=CARTESIAN_POINT ( 'NONE',  ( 28.49999999999980460, 16.77039438581781639, 0.4657186855307072215 ) ) ;
#228=LINE ( 'NONE', #88730, #91900 ) ;
#230=DIRECTION ( 'NONE',  ( -0.7071067811865486830, -0.7071067811865464625, 0.000000000000000000 ) ) ;
#231=CARTESIAN_POINT ( 'NONE',  ( 5.343289998337836799, 3.759292476615681888, 13.27625715073266832 ) ) ;
#232=ORIENTED_EDGE ( 'NONE', *, *, #94046, .F. ) ;
#233=DIRECTION ( 'NONE',  ( 0.7071067811865487940, -0.7071067811865463515, 0.000000000000000000 ) ) ;
#234=EDGE_LOOP ( 'NONE', ( #55561, #105143, #26118, #111519 ) ) ;
#235=EDGE_CURVE ( 'NONE', #55527, #138159, #86292, .T. ) ;
#236=EDGE_CURVE ( 'NONE', #105061, #6978, #28339, .T. ) ;
#239=ORIENTED_EDGE ( 'NONE', *, *, #100908, .T. ) ;
#240=CARTESIAN_POINT ( 'NONE',  ( -34.92500000000001137, -22.22500000000000142, 4.000000000000000000 ) ) ;
#241=EDGE_CURVE ( 'NONE', #93680, #60629, #40644, .T. ) ;
#242=VECTOR ( 'NONE', #139566, 1000.000000000000000 ) ;
#243=CARTESIAN_POINT ( 'NONE',  ( -14.99999999999990230, 11.58746187583913390, 4.000000000000000000 ) ) ;
#245=EDGE_CURVE ( 'NONE', #60766, #87872, #129054, .T. ) ;
#246=ORIENTED_EDGE ( 'NONE', *, *, #38962, .T. ) ;
#247=CARTESIAN_POINT ( 'NONE',  ( -57.29974487139158157, -27.71228299555246011, 4.000000000000000000 ) ) ;
#249=VECTOR ( 'NONE', #124185, 999.9999999999998863 ) ;
#250=LINE ( 'NONE', #99570, #21719 ) ;
#251=FACE_OUTER_BOUND ( 'NONE', #30396, .T. ) ;
#252=EDGE_CURVE ( 'NONE', #89926, #37388, #72601, .T. ) ;
#253=AXIS2_PLACEMENT_3D ( 'NONE', #31106, #7884, #115919 ) ;
#254=CARTESIAN_POINT ( 'NONE',  ( 0.000000000000000000, 0.000000000000000000, 5.000000000000000000 ) ) ;
#255=DIRECTION ( 'NONE',  ( -0.3543493200069163240, 0.000000000000000000, 0.9351131265310288487 ) ) ;
#256=DIRECTION ( 'NONE',  ( 0.7071067811865487940, -0.7071067811865463515, 0.000000000000000000 ) ) ;
#257=AXIS2_PLACEMENT_3D ( 'NONE', #43444, #11484, #76815 ) ;
#258=CARTESIAN_POINT ( 'NONE',  ( -11.51078643762690490, -27.52281430457047406, 5.000000000000000000 ) ) ;
#260=ORIENTED_EDGE ( 'NONE', *, *, #110078, .F. ) ;
#262=ORIENTED_EDGE ( 'NONE', *, *, #76274, .T. ) ;
#263=VECTOR ( 'NONE', #104295, 1000.000000000000000 ) ;
#264=CARTESIAN_POINT ( 'NONE',  ( 14.20710678118644665, 6.759292476615645029, 5.000000000000000000 ) ) ;
#265=EDGE_CURVE ( 'NONE', #60839, #128811, #85538, .T. ) ;
#266=ORIENTED_EDGE ( 'NONE', *, *, #113885, .F. ) ;
#267=ORIENTED_EDGE ( 'NONE', *, *, #56927, .F. ) ;
#268=VECTOR ( 'NONE', #71889, 999.9999999999998863 ) ;
#270=VERTEX_POINT ( 'NONE', #52214 ) ;
#272=CARTESIAN_POINT ( 'NONE',  ( 18.32816939922340183, -6.740707523384209310, 4.000000000000000000 ) ) ;
#275=CARTESIAN_POINT ( 'NONE',  ( -23.51078643762690490, -27.52281430457038880, 5.000000000000000000 ) ) ;
#276=ORIENTED_EDGE ( 'NONE', *, *, #16957, .T. ) ;
#277=LINE ( 'NONE', #122073, #61918 ) ;
#279=DIRECTION ( 'NONE',  ( -0.000000000000000000, -0.3543493200069152693, 0.9351131265310292928 ) ) ;
#280=DIRECTION ( 'NONE',  ( -0.6830127018922180770, -0.6830127018922204085, -0.2588190451025213501 ) ) ;
#281=DIRECTION ( 'NONE',  ( 0.7071067811865486830, -0.7071067811865464625, -0.000000000000000000 ) ) ;
#282=EDGE_LOOP ( 'NONE', ( #75330, #107556, #58149, #92149 ) ) ;
#283=VECTOR ( 'NONE', #27809, 1000.000000000000000 ) ;
#284=ORIENTED_EDGE ( 'NONE', *, *, #109477, .T. ) ;
#285=FACE_OUTER_BOUND ( 'NONE', #1360, .T. ) ;
#286=LINE ( 'NONE', #34381, #116352 ) ;
#287=CARTESIAN_POINT ( 'NONE',  ( 1.171830600776462061, -20.24070752338407786, 4.000000000000000000 ) ) ;
#288=VERTEX_POINT ( 'NONE', #119584 ) ;
#289=CARTESIAN_POINT ( 'NONE',  ( -72.48921356237309510, -27.52281430457106026, 5.000000000000000000 ) ) ;
#290=DIRECTION ( 'NONE',  ( -0.6830127018922180770, -0.6830127018922204085, -0.2588190451025213501 ) ) ;
#291=ORIENTED_EDGE ( 'NONE', *, *, #84770, .T. ) ;
#292=VECTOR ( 'NONE', #30348, 1000.000000000000000 ) ;
#293=EDGE_CURVE ( 'NONE', #72640, #57817, #29041, .T. ) ;
#294=LINE ( 'NONE', #88788, #58847 ) ;
#295=LINE ( 'NONE', #101775, #132017 ) ;
#296=CARTESIAN_POINT ( 'NONE',  ( -15.48921356237309510, -27.52281430457066236, 5.000000000000000000 ) ) ;
#297=AXIS2_PLACEMENT_3D ( 'NONE', #93929, #83070, #52567 ) ;
#299=EDGE_CURVE ( 'NONE', #18521, #55587, #117446, .T. ) ;
#301=FACE_OUTER_BOUND ( 'NONE', #7948, .T. ) ;
#302=LINE ( 'NONE', #112664, #34486 ) ;
#303=ORIENTED_EDGE ( 'NONE', *, *, #124962, .T. ) ;
#305=VERTEX_POINT ( 'NONE', #7974 ) ;
#309=EDGE_CURVE ( 'NONE', #55336, #42777, #64521, .T. ) ;
#310=LINE ( 'NONE', #120669, #138798 ) ;
#312=PLANE ( 'NONE',  #122563 ) ;
#313=DIRECTION ( 'NONE',  ( -0.3543493200069162685, -0.000000000000000000, -0.9351131265310288487 ) ) ;
#314=CARTESIAN_POINT ( 'NONE',  ( -21.70710678118638981, 11.25929247661560773, 5.000000000000000000 ) ) ;
#317=LINE ( 'NONE', #143165, #97408 ) ;
#318=LINE ( 'NONE', #11922, #100246 ) ;
#319=CARTESIAN_POINT ( 'NONE',  ( 12.48921356237309155, -27.52281430457064104, 5.000000000000000000 ) ) ;
#320=AXIS2_PLACEMENT_3D ( 'NONE', #30283, #118710, #19405 ) ;
#321=DIRECTION ( 'NONE',  ( 0.7071067811865486830, -0.7071067811865464625, -0.000000000000000000 ) ) ;
#323=CARTESIAN_POINT ( 'NONE',  ( 60.48921356237309510, -27.52281430457097500, 5.000000000000000000 ) ) ;
#324=VECTOR ( 'NONE', #96544, 1000.000000000000000 ) ;
#325=( BOUNDED_CURVE ( )  B_SPLINE_CURVE ( 3, ( #134781, #78969, #34023, #14395 ),
 .UNSPECIFIED., .F., .T. ) 
 B_SPLINE_CURVE_WITH_KNOTS ( ( 4, 4 ),
 ( 4.350170835173023498, 4.500739107949261353 ),
 .UNSPECIFIED. ) 
 CURVE ( )  GEOMETRIC_REPRESENTATION_ITEM ( )  RATIONAL_B_SPLINE_CURVE ( ( 1.000000000000000000, 0.9981116584018945304, 0.9981116584018945304, 1.000000000000000000 ) ) 
 REPRESENTATION_ITEM ( '' )  );
#326=AXIS2_PLACEMENT_3D ( 'NONE', #113465, #122938, #69282 ) ;
#330=VERTEX_POINT ( 'NONE', #9384 ) ;
#332=VERTEX_POINT ( 'NONE', #53661 ) ;
#333=VECTOR ( 'NONE', #70121, 1000.000000000000000 ) ;
#334=VECTOR ( 'NONE', #77445, 1000.000000000000000 ) ;
#336=CARTESIAN_POINT ( 'NONE',  ( 8.816011393731004731, 28.73617430169781173, 5.000000000000000000 ) ) ;
#337=AXIS2_PLACEMENT_3D ( 'NONE', #92579, #128791, #104900 ) ;
#338=PLANE ( 'NONE',  #138048 ) ;
#339=AXIS2_PLACEMENT_3D ( 'NONE', #38488, #104434, #126890 ) ;
#340=FACE_OUTER_BOUND ( 'NONE', #82107, .T. ) ;
#341=PLANE ( 'NONE',  #25712 ) ;
#342=PLANE ( 'NONE',  #141146 ) ;
#343=EDGE_CURVE ( 'NONE', #92701, #118319, #97869, .T. ) ;
#344=CARTESIAN_POINT ( 'NONE',  ( -34.42500000000001137, 13.54139925780187603, 5.000000000000000000 ) ) ;
#345=CARTESIAN_POINT ( 'NONE',  ( -34.42500000000001137, 0.000000000000000000, 4.500000000000000888 ) ) ;
#346=EDGE_CURVE ( 'NONE', #132444, #99209, #109450, .T. ) ;
#347=ORIENTED_EDGE ( 'NONE', *, *, #6469, .T. ) ;
#348=ORIENTED_EDGE ( 'NONE', *, *, #75130, .F. ) ;
#349=FACE_OUTER_BOUND ( 'NONE', #74753, .T. ) ;
#350=FACE_OUTER_BOUND ( 'NONE', #24729, .T. ) ;
#351=VECTOR ( 'NONE', #98125, 1000.000000000000000 ) ;
#352=CARTESIAN_POINT ( 'NONE',  ( -24.18398860626899705, 28.73617430169804265, 5.000000000000000000 ) ) ;
#353=DIRECTION ( 'NONE',  ( -0.6830127018922181881, 0.6830127018922202975, -0.2588190451025214056 ) ) ;
#355=CARTESIAN_POINT ( 'NONE',  ( -11.29289321881337571, 17.25929247661553489, 5.000000000000000000 ) ) ;
#356=ADVANCED_FACE ( 'NONE', ( #123207 ), #110146, .T. ) ;
#358=VERTEX_POINT ( 'NONE', #56560 ) ;
#360=VECTOR ( 'NONE', #90136, 1000.000000000000000 ) ;
#361=CARTESIAN_POINT ( 'NONE',  ( 5.999999999999960032, 18.08204922493374411, 0.9627537363044759156 ) ) ;
#362=DIRECTION ( 'NONE',  ( 0.7071067811865487940, 0.7071067811865463515, 0.000000000000000000 ) ) ;
#363=ORIENTED_EDGE ( 'NONE', *, *, #24956, .F. ) ;
#364=EDGE_CURVE ( 'NONE', #108536, #57879, #101424, .T. ) ;
#366=DIRECTION ( 'NONE',  ( -0.7071067811865487940, 0.7071067811865463515, -0.000000000000000000 ) ) ;
#367=ORIENTED_EDGE ( 'NONE', *, *, #20533, .T. ) ;
#368=AXIS2_PLACEMENT_3D ( 'NONE', #120768, #21477, #143248 ) ;
#373=VERTEX_POINT ( 'NONE', #76859 ) ;
#374=VECTOR ( 'NONE', #35742, 1000.000000000000000 ) ;
#375=CARTESIAN_POINT ( 'NONE',  ( -24.32816939922336275, 14.25929247661557575, 4.000000000000000000 ) ) ;
#376=DIRECTION ( 'NONE',  ( -0.7071067811865486830, -0.7071067811865464625, 0.000000000000000000 ) ) ;
#378=CARTESIAN_POINT ( 'NONE',  ( 0.3281693992235297785, 17.25929247661554200, 4.000000000000000000 ) ) ;
#381=CARTESIAN_POINT ( 'NONE',  ( -2.999999999999975131, -6.033600742197674727, 5.000000000000000000 ) ) ;
#382=ORIENTED_EDGE ( 'NONE', *, *, #28958, .T. ) ;
#383=CARTESIAN_POINT ( 'NONE',  ( -2.999999999999976463, -1.068876922607804314, 4.000000000000000000 ) ) ;
#384=CARTESIAN_POINT ( 'NONE',  ( 2.218373117075048029, 21.74787736706806385, 4.999607392498048419 ) ) ;
#385=CARTESIAN_POINT ( 'NONE',  ( -23.99451991528749062, 28.92564299267954908, 4.000000000000000000 ) ) ;
#386=AXIS2_PLACEMENT_3D ( 'NONE', #58460, #98177, #96016 ) ;
#388=ORIENTED_EDGE ( 'NONE', *, *, #12820, .F. ) ;
#389=ORIENTED_EDGE ( 'NONE', *, *, #16681, .T. ) ;
#391=VERTEX_POINT ( 'NONE', #65987 ) ;
#392=CARTESIAN_POINT ( 'NONE',  ( -34.92500000000001137, 22.22500000000000142, 4.000000000000000000 ) ) ;
#393=CARTESIAN_POINT ( 'NONE',  ( -26.29289321881326558, -9.740707523384184441, 5.000000000000000000 ) ) ;
#394=DIRECTION ( 'NONE',  ( 0.7071067811865487940, 0.7071067811865463515, 0.000000000000000000 ) ) ;
#396=CARTESIAN_POINT ( 'NONE',  ( -24.98480450340313652, 2.536990198832462351, 5.000000000000000000 ) ) ;
#397=CARTESIAN_POINT ( 'NONE',  ( 17.29289321881334018, -6.740707523384209310, 5.000000000000000000 ) ) ;
#398=VERTEX_POINT ( 'NONE', #23880 ) ;
#399=ORIENTED_EDGE ( 'NONE', *, *, #4654, .T. ) ;
#400=VECTOR ( 'NONE', #70487, 1000.000000000000000 ) ;
#401=DIRECTION ( 'NONE',  ( -0.7071067811865486830, -0.7071067811865464625, 0.000000000000000000 ) ) ;
#403=ORIENTED_EDGE ( 'NONE', *, *, #107919, .F. ) ;
#404=LINE ( 'NONE', #133118, #125414 ) ;
#405=EDGE_CURVE ( 'NONE', #121029, #128151, #88328, .T. ) ;
#406=FACE_OUTER_BOUND ( 'NONE', #46336, .T. ) ;
#407=FACE_OUTER_BOUND ( 'NONE', #98667, .T. ) ;
#409=ORIENTED_EDGE ( 'NONE', *, *, #43363, .T. ) ;
#410=FACE_BOUND ( 'NONE', #51809, .T. ) ;
#411=CARTESIAN_POINT ( 'NONE',  ( -3.005480084712505828, 28.92564299267936079, 4.000000000000000000 ) ) ;
#413=CARTESIAN_POINT ( 'NONE',  ( -18.29974487139159223, -27.71228299555219010, 4.000000000000000000 ) ) ;
#414=CARTESIAN_POINT ( 'NONE',  ( -7.499999999999951150, 13.08746187583912146, 4.000000000000000000 ) ) ;
#415=LINE ( 'NONE', #88909, #141470 ) ;
#416=ORIENTED_EDGE ( 'NONE', *, *, #6486, .F. ) ;
#417=EDGE_CURVE ( 'NONE', #27268, #65916, #67404, .T. ) ;
#418=ORIENTED_EDGE ( 'NONE', *, *, #36030, .F. ) ;
#420=ORIENTED_EDGE ( 'NONE', *, *, #111228, .F. ) ;
#421=EDGE_CURVE ( 'NONE', #133840, #42748, #31897, .T. ) ;
#423=ORIENTED_EDGE ( 'NONE', *, *, #120728, .F. ) ;
#424=ADVANCED_FACE ( 'NONE', ( #143502 ), #11532, .F. ) ;
#425=CARTESIAN_POINT ( 'NONE',  ( 9.707106781186480404, -0.7407075233842735917, 5.000000000000000000 ) ) ;
#426=VECTOR ( 'NONE', #53827, 1000.000000000000000 ) ;
#427=EDGE_CURVE ( 'NONE', #3647, #106547, #19837, .T. ) ;
#429=DIRECTION ( 'NONE',  ( -0.3543493200069162685, -0.000000000000000000, -0.9351131265310288487 ) ) ;
#430=VECTOR ( 'NONE', #23278, 999.9999999999998863 ) ;
#431=VECTOR ( 'NONE', #87814, 1000.000000000000000 ) ;
#432=CARTESIAN_POINT ( 'NONE',  ( 39.29974487139159578, -27.71228299555233576, 4.000000000000000000 ) ) ;
#433=EDGE_LOOP ( 'NONE', ( #100677, #114743, #113008 ) ) ;
#434=DIRECTION ( 'NONE',  ( 0.7071067811865487940, 0.7071067811865463515, 0.000000000000000000 ) ) ;
#435=DIRECTION ( 'NONE',  ( -0.7071067811865487940, 0.7071067811865463515, -0.000000000000000000 ) ) ;
#436=CARTESIAN_POINT ( 'NONE',  ( 8.999999999999943157, 7.552185695429089130, 5.000000000000000000 ) ) ;
#441=VECTOR ( 'NONE', #51936, 1000.000000000000000 ) ;
#442=VECTOR ( 'NONE', #49067, 1000.000000000000000 ) ;
#444=DIRECTION ( 'NONE',  ( 0.3543493200069162685, -0.000000000000000000, -0.9351131265310288487 ) ) ;
#445=VERTEX_POINT ( 'NONE', #6784 ) ;
#447=DIRECTION ( 'NONE',  ( 0.6830127018922180770, -0.6830127018922204085, -0.2588190451025213501 ) ) ;
#448=EDGE_CURVE ( 'NONE', #139414, #35675, #74241, .T. ) ;
#449=ORIENTED_EDGE ( 'NONE', *, *, #79627, .F. ) ;
#450=EDGE_LOOP ( 'NONE', ( #37770, #449, #12481, #125 ) ) ;
#451=EDGE_CURVE ( 'NONE', #68140, #73925, #41598, .T. ) ;
#454=EDGE_LOOP ( 'NONE', ( #116566, #36964, #17088, #40231, #105946, #55816 ) ) ;
#455=EDGE_CURVE ( 'NONE', #121396, #35500, #128617, .T. ) ;
#456=PLANE ( 'NONE',  #41905 ) ;
#459=CYLINDRICAL_SURFACE ( 'NONE', #21662, 0.5000000000000004441 ) ;
#460=ORIENTED_EDGE ( 'NONE', *, *, #37283, .F. ) ;
#461=DIRECTION ( 'NONE',  ( -0.000000000000000000, -0.3543493200069152693, 0.9351131265310292928 ) ) ;
#462=LINE ( 'NONE', #141906, #37760 ) ;
#463=ORIENTED_EDGE ( 'NONE', *, *, #82126, .T. ) ;
#465=AXIS2_PLACEMENT_3D ( 'NONE', #68774, #78939, #1320 ) ;
#466=PLANE ( 'NONE',  #66047 ) ;
#467=VERTEX_POINT ( 'NONE', #51789 ) ;
#468=AXIS2_PLACEMENT_3D ( 'NONE', #89931, #34153, #23234 ) ;
#469=DIRECTION ( 'NONE',  ( 1.000000000000000000, 0.000000000000000000, 0.000000000000000000 ) ) ;
#470=DIRECTION ( 'NONE',  ( -0.7071067811865486830, 0.7071067811865464625, 0.000000000000000000 ) ) ;
#471=ORIENTED_EDGE ( 'NONE', *, *, #95394, .T. ) ;
#472=AXIS2_PLACEMENT_3D ( 'NONE', #141340, #42773, #52189 ) ;
#474=VERTEX_POINT ( 'NONE', #29291 ) ;
#475=EDGE_CURVE ( 'NONE', #12429, #109431, #7525, .T. ) ;
#477=VECTOR ( 'NONE', #71928, 1000.000000000000227 ) ;
#478=LINE ( 'NONE', #33862, #127907 ) ;
#479=CARTESIAN_POINT ( 'NONE',  ( 34.92499999999998295, 13.70193056682084887, 4.500000000000000888 ) ) ;
#480=ORIENTED_EDGE ( 'NONE', *, *, #67194, .T. ) ;
#481=CARTESIAN_POINT ( 'NONE',  ( -16.49999999999988276, -13.53360074219760101, 5.000000000000000000 ) ) ;
#482=VERTEX_POINT ( 'NONE', #31451 ) ;
#483=VECTOR ( 'NONE', #57375, 1000.000000000000227 ) ;
#485=PLANE ( 'NONE',  #101778 ) ;
#488=VERTEX_POINT ( 'NONE', #75673 ) ;
#489=VERTEX_POINT ( 'NONE', #100278 ) ;
#490=ADVANCED_FACE ( 'NONE', ( #66231 ), #198, .F. ) ;
#491=VECTOR ( 'NONE', #127188, 1000.000000000000000 ) ;
#492=ORIENTED_EDGE ( 'NONE', *, *, #81875, .T. ) ;
#493=PLANE ( 'NONE',  #37151 ) ;
#494=CARTESIAN_POINT ( 'NONE',  ( 39.29974487139159578, -27.71228299555233576, 4.000000000000000000 ) ) ;
#495=VECTOR ( 'NONE', #102903, 1000.000000000000114 ) ;
#497=CARTESIAN_POINT ( 'NONE',  ( -23.99999999999983302, 16.93112307739201583, 4.000000000000000000 ) ) ;
#498=CARTESIAN_POINT ( 'NONE',  ( -14.24890464969599435, -0.3792994071806680689, 4.162343009174984232 ) ) ;
#499=DIRECTION ( 'NONE',  ( -0.3543493200069162685, -0.000000000000000000, -0.9351131265310288487 ) ) ;
#501=LINE ( 'NONE', #20833, #42091 ) ;
#502=DIRECTION ( 'NONE',  ( -0.7071067811865486830, 0.7071067811865464625, 0.000000000000000000 ) ) ;
#503=ORIENTED_EDGE ( 'NONE', *, *, #122198, .F. ) ;
#504=CARTESIAN_POINT ( 'NONE',  ( -41.99451991528749062, 28.92564299267967343, 4.000000000000000000 ) ) ;
#505=VECTOR ( 'NONE', #41332, 1000.000000000000000 ) ;
#506=EDGE_LOOP ( 'NONE', ( #140030, #45972, #39854, #108702 ) ) ;
#507=CARTESIAN_POINT ( 'NONE',  ( 57.18398860626899705, 28.73617430169827358, 5.000000000000000000 ) ) ;
#508=ORIENTED_EDGE ( 'NONE', *, *, #48578, .F. ) ;
#509=CARTESIAN_POINT ( 'NONE',  ( -48.48921356237309510, -27.52281430457089328, 5.000000000000000000 ) ) ;
#510=CARTESIAN_POINT ( 'NONE',  ( -48.48921356237309510, -27.52281430457089328, 5.000000000000000000 ) ) ;
#511=ORIENTED_EDGE ( 'NONE', *, *, #137999, .F. ) ;
#512=EDGE_CURVE ( 'NONE', #80329, #53800, #11805, .T. ) ;
#513=DIRECTION ( 'NONE',  ( -0.7071067811865487940, 0.7071067811865463515, -0.000000000000000000 ) ) ;
#514=LINE ( 'NONE', #1914, #14794 ) ;
#515=ORIENTED_EDGE ( 'NONE', *, *, #127473, .F. ) ;
#516=CARTESIAN_POINT ( 'NONE',  ( -15.18398860626900237, 28.73617430169797871, 5.000000000000000000 ) ) ;
#517=AXIS2_PLACEMENT_3D ( 'NONE', #20502, #1596, #109680 ) ;
#519=DIRECTION ( 'NONE',  ( -0.7071067811865487940, 0.7071067811865463515, -0.000000000000000000 ) ) ;
#520=ORIENTED_EDGE ( 'NONE', *, *, #112530, .T. ) ;
#521=LINE ( 'NONE', #89005, #45331 ) ;
#525=DIRECTION ( 'NONE',  ( 0.7071067811865487940, 0.7071067811865463515, 0.000000000000000000 ) ) ;
#527=LINE ( 'NONE', #44069, #11340 ) ;
#529=DIRECTION ( 'NONE',  ( -0.7071067811865486830, -0.7071067811865464625, 0.000000000000000000 ) ) ;
#530=VECTOR ( 'NONE', #99105, 999.9999999999998863 ) ;
#531=VECTOR ( 'NONE', #90557, 1000.000000000000000 ) ;
#534=LINE ( 'NONE', #75981, #91767 ) ;
#535=ORIENTED_EDGE ( 'NONE', *, *, #15196, .F. ) ;
#536=VERTEX_POINT ( 'NONE', #86555 ) ;
#537=AXIS2_PLACEMENT_3D ( 'NONE', #63476, #8301, #7604 ) ;
#539=CARTESIAN_POINT ( 'NONE',  ( 27.70710678118635073, -12.74070752338415424, 5.000000000000000000 ) ) ;
#540=VERTEX_POINT ( 'NONE', #130787 ) ;
#541=ADVANCED_FACE ( 'NONE', ( #99530 ), #56092, .F. ) ;
#543=LINE ( 'NONE', #123072, #77852 ) ;
#544=LINE ( 'NONE', #44839, #9237 ) ;
#545=AXIS2_PLACEMENT_3D ( 'NONE', #123467, #24124, #58230 ) ;
#546=CARTESIAN_POINT ( 'NONE',  ( -34.49999999999975842, -7.535744391599424219, 4.994342998332167660 ) ) ;
#547=VECTOR ( 'NONE', #85064, 1000.000000000000000 ) ;
#548=CARTESIAN_POINT ( 'NONE',  ( 0.000000000000000000, 0.000000000000000000, 5.000000000000000000 ) ) ;
#550=LINE ( 'NONE', #133943, #31321 ) ;
#552=CARTESIAN_POINT ( 'NONE',  ( 21.32816939922336985, -15.74070752338412760, 4.000000000000000000 ) ) ;
#553=EDGE_CURVE ( 'NONE', #52608, #118518, #64800, .T. ) ;
#554=CARTESIAN_POINT ( 'NONE',  ( 34.49999999999975131, 22.21934299833216642, 4.348028800457638177 ) ) ;
#556=CARTESIAN_POINT ( 'NONE',  ( -24.70710678118637205, 8.259292476615636147, 5.000000000000000000 ) ) ;
#557=FACE_OUTER_BOUND ( 'NONE', #112855, .T. ) ;
#562=CARTESIAN_POINT ( 'NONE',  ( 47.99451991528749062, 28.92564299267971251, 4.000000000000000000 ) ) ;
#563=CARTESIAN_POINT ( 'NONE',  ( 3.707106781186515487, -15.74070752338412404, 5.000000000000000000 ) ) ;
#564=ORIENTED_EDGE ( 'NONE', *, *, #87957, .F. ) ;
#565=ORIENTED_EDGE ( 'NONE', *, *, #54246, .F. ) ;
#566=VERTEX_POINT ( 'NONE', #32907 ) ;
#568=ORIENTED_EDGE ( 'NONE', *, *, #120751, .T. ) ;
#569=DIRECTION ( 'NONE',  ( 0.7071067811865487940, -0.7071067811865463515, 0.000000000000000000 ) ) ;
#571=CARTESIAN_POINT ( 'NONE',  ( -17.99451991528748351, 28.92564299267950645, 4.000000000000000000 ) ) ;
#572=CARTESIAN_POINT ( 'NONE',  ( 0.000000000000000000, 0.000000000000000000, 5.000000000000000000 ) ) ;
#574=EDGE_CURVE ( 'NONE', #120024, #43089, #22666, .T. ) ;
#575=CARTESIAN_POINT ( 'NONE',  ( 20.99999999999985079, -16.06887692260765377, 4.000000000000000000 ) ) ;
#579=ORIENTED_EDGE ( 'NONE', *, *, #10590, .F. ) ;
#580=VECTOR ( 'NONE', #117247, 1000.000000000000227 ) ;
#581=LINE ( 'NONE', #108604, #83736 ) ;
#582=PLANE ( 'NONE',  #88617 ) ;
#583=VECTOR ( 'NONE', #73522, 1000.000000000000227 ) ;
#584=AXIS2_PLACEMENT_3D ( 'NONE', #45025, #34830, #21796 ) ;
#585=EDGE_LOOP ( 'NONE', ( #84587, #117927, #110585, #17558 ) ) ;
#586=ORIENTED_EDGE ( 'NONE', *, *, #664, .T. ) ;
#588=FACE_OUTER_BOUND ( 'NONE', #75692, .T. ) ;
#589=CARTESIAN_POINT ( 'NONE',  ( 5.700255128608413102, -27.71228299555201957, 4.000000000000000000 ) ) ;
#593=CARTESIAN_POINT ( 'NONE',  ( 26.99999999999980815, 10.21212019023811557, -2.019456568337861135 ) ) ;
#594=EDGE_CURVE ( 'NONE', #43234, #102340, #12534, .T. ) ;
#595=LINE ( 'NONE', #67318, #59027 ) ;
#596=ADVANCED_FACE ( 'NONE', ( #108976 ), #23407, .F. ) ;
#597=ORIENTED_EDGE ( 'NONE', *, *, #82825, .T. ) ;
#598=ORIENTED_EDGE ( 'NONE', *, *, #22116, .T. ) ;
#599=EDGE_CURVE ( 'NONE', #53838, #27206, #43053, .T. ) ;
#600=CARTESIAN_POINT ( 'NONE',  ( -2.671830600776458287, 5.259292476615669010, 4.000000000000000000 ) ) ;
#601=ORIENTED_EDGE ( 'NONE', *, *, #119460, .T. ) ;
#602=ORIENTED_EDGE ( 'NONE', *, *, #80662, .F. ) ;
#603=AXIS2_PLACEMENT_3D ( 'NONE', #111128, #114010, #68409 ) ;
#604=EDGE_CURVE ( 'NONE', #29147, #103671, #114246, .T. ) ;
#605=EDGE_CURVE ( 'NONE', #107763, #100224, #143057, .T. ) ;
#606=CARTESIAN_POINT ( 'NONE',  ( -9.183988606268997046, 28.73617430169793607, 5.000000000000000000 ) ) ;
#607=ORIENTED_EDGE ( 'NONE', *, *, #61214, .T. ) ;
#608=CARTESIAN_POINT ( 'NONE',  ( -11.67183060077639212, -3.740707523384244837, 4.000000000000000000 ) ) ;
#609=CARTESIAN_POINT ( 'NONE',  ( -4.110173228882081808, -22.22499999999999787, 4.785647885939356527 ) ) ;
#610=CARTESIAN_POINT ( 'NONE',  ( 34.45011844616451668, -19.48371918836231131, 5.000000000000000888 ) ) ;
#611=CARTESIAN_POINT ( 'NONE',  ( 0.000000000000000000, 0.000000000000000000, 5.000000000000000000 ) ) ;
#612=VECTOR ( 'NONE', #14332, 1000.000000000000000 ) ;
#613=LINE ( 'NONE', #33988, #72153 ) ;
#614=ORIENTED_EDGE ( 'NONE', *, *, #124518, .T. ) ;
#615=EDGE_CURVE ( 'NONE', #122922, #20850, #37895, .T. ) ;
#616=ORIENTED_EDGE ( 'NONE', *, *, #111910, .T. ) ;
#617=PLANE ( 'NONE',  #31847 ) ;
#619=LINE ( 'NONE', #111537, #97830 ) ;
#620=EDGE_CURVE ( 'NONE', #75539, #80902, #91546, .T. ) ;
#621=ORIENTED_EDGE ( 'NONE', *, *, #448, .T. ) ;
#622=CARTESIAN_POINT ( 'NONE',  ( 84.18398860626899705, 28.73617430169846187, 5.000000000000000000 ) ) ;
#623=ORIENTED_EDGE ( 'NONE', *, *, #73535, .T. ) ;
#624=EDGE_LOOP ( 'NONE', ( #65991, #135134, #38337 ) ) ;
#625=VECTOR ( 'NONE', #10022, 1000.000000000000000 ) ;
#626=VERTEX_POINT ( 'NONE', #16070 ) ;
#627=EDGE_CURVE ( 'NONE', #673, #24426, #48759, .T. ) ;
#628=DIRECTION ( 'NONE',  ( 0.7071067811865487940, -0.7071067811865463515, 0.000000000000000000 ) ) ;
#629=DIRECTION ( 'NONE',  ( 0.7071067811865486830, -0.7071067811865464625, -0.000000000000000000 ) ) ;
#630=CARTESIAN_POINT ( 'NONE',  ( 29.20710678118634718, -5.240707523384230626, 5.000000000000000000 ) ) ;
#632=CARTESIAN_POINT ( 'NONE',  ( 30.48921356237309510, -27.52281430457076894, 5.000000000000000000 ) ) ;
#633=CARTESIAN_POINT ( 'NONE',  ( 13.82816939922344091, 6.759292476615649470, 4.000000000000000000 ) ) ;
#636=VECTOR ( 'NONE', #35690, 999.9999999999998863 ) ;
#637=PLANE ( 'NONE',  #65519 ) ;
#639=VECTOR ( 'NONE', #108295, 1000.000000000000000 ) ;
#641=ORIENTED_EDGE ( 'NONE', *, *, #126480, .F. ) ;
#642=DIRECTION ( 'NONE',  ( -0.7071067811865486830, -0.7071067811865464625, 0.000000000000000000 ) ) ;
#643=FACE_OUTER_BOUND ( 'NONE', #70966, .T. ) ;
#645=VERTEX_POINT ( 'NONE', #82129 ) ;
#647=EDGE_CURVE ( 'NONE', #93537, #97071, #26987, .T. ) ;
#649=AXIS2_PLACEMENT_3D ( 'NONE', #98295, #41049, #75831 ) ;
#652=CARTESIAN_POINT ( 'NONE',  ( 36.18398860626899705, 28.73617430169812437, 5.000000000000000000 ) ) ;
#653=ORIENTED_EDGE ( 'NONE', *, *, #128854, .T. ) ;
#654=ORIENTED_EDGE ( 'NONE', *, *, #99886, .F. ) ;
#655=CARTESIAN_POINT ( 'NONE',  ( -8.050415908692611922, -22.22500000000000142, 15.18378453690488072 ) ) ;
#657=DIRECTION ( 'NONE',  ( -0.6830127018922181881, 0.6830127018922202975, -0.2588190451025214056 ) ) ;
#658=CARTESIAN_POINT ( 'NONE',  ( 42.48921356237308800, -27.52281430457085065, 5.000000000000000000 ) ) ;
#659=EDGE_CURVE ( 'NONE', #13443, #108133, #113272, .T. ) ;
#660=ORIENTED_EDGE ( 'NONE', *, *, #55307, .T. ) ;
#661=LINE ( 'NONE', #43469, #58016 ) ;
#663=FACE_OUTER_BOUND ( 'NONE', #7412, .T. ) ;
#664=EDGE_CURVE ( 'NONE', #70961, #59222, #36447, .T. ) ;
#667=VERTEX_POINT ( 'NONE', #3090 ) ;
#671=ORIENTED_EDGE ( 'NONE', *, *, #119679, .F. ) ;
#673=VERTEX_POINT ( 'NONE', #57504 ) ;
#674=FACE_OUTER_BOUND ( 'NONE', #8826, .T. ) ;
#676=PLANE ( 'NONE',  #72895 ) ;
#677=CARTESIAN_POINT ( 'NONE',  ( 20.99999999999985079, -6.108550654416941228, -3.114665004254919101 ) ) ;
#678=ORIENTED_EDGE ( 'NONE', *, *, #11186, .F. ) ;
#680=LINE ( 'NONE', #44973, #51290 ) ;
#681=LINE ( 'NONE', #79745, #4821 ) ;
#683=PLANE ( 'NONE',  #37383 ) ;
#684=DIRECTION ( 'NONE',  ( 0.7071067811865487940, 0.7071067811865463515, 0.000000000000000000 ) ) ;
#685=EDGE_LOOP ( 'NONE', ( #90796, #60174, #71280, #138128 ) ) ;
#686=LINE ( 'NONE', #132693, #50983 ) ;
#687=VERTEX_POINT ( 'NONE', #80678 ) ;
#688=ORIENTED_EDGE ( 'NONE', *, *, #99468, .T. ) ;
#689=CARTESIAN_POINT ( 'NONE',  ( 21.48921356237309155, -27.52281430457070499, 5.000000000000000000 ) ) ;
#690=LINE ( 'NONE', #131960, #52937 ) ;
#691=ORIENTED_EDGE ( 'NONE', *, *, #94261, .T. ) ;
#693=VECTOR ( 'NONE', #63519, 1000.000000000000000 ) ;
#694=CARTESIAN_POINT ( 'NONE',  ( -2.510786437626908008, -27.52281430457053446, 5.000000000000000000 ) ) ;
#695=CARTESIAN_POINT ( 'NONE',  ( 0.000000000000000000, 0.000000000000000000, 5.000000000000000000 ) ) ;
#696=CARTESIAN_POINT ( 'NONE',  ( -15.48921356237309510, -27.52281430457066236, 5.000000000000000000 ) ) ;
#699=VECTOR ( 'NONE', #102639, 1000.000000000000227 ) ;
#700=PLANE ( 'NONE',  #109644 ) ;
#701=LINE ( 'NONE', #44997, #59943 ) ;
#703=DIRECTION ( 'NONE',  ( -0.000000000000000000, 0.3543493200069152138, -0.9351131265310292928 ) ) ;
#705=CARTESIAN_POINT ( 'NONE',  ( 12.18398860626900060, 28.73617430169795739, 5.000000000000000000 ) ) ;
#706=CARTESIAN_POINT ( 'NONE',  ( 66.18398860626901126, 28.73617430169833753, 5.000000000000000000 ) ) ;
#707=FACE_OUTER_BOUND ( 'NONE', #88184, .T. ) ;
#708=EDGE_LOOP ( 'NONE', ( #23324, #103090, #25830, #73276 ) ) ;
#709=EDGE_LOOP ( 'NONE', ( #127924, #22174, #9037, #2696 ) ) ;
#711=ORIENTED_EDGE ( 'NONE', *, *, #130086, .T. ) ;
#712=ORIENTED_EDGE ( 'NONE', *, *, #38638, .T. ) ;
#713=ORIENTED_EDGE ( 'NONE', *, *, #40905, .F. ) ;
#714=CARTESIAN_POINT ( 'NONE',  ( -15.18398860626900237, 28.73617430169797871, 5.000000000000000000 ) ) ;
#715=FACE_OUTER_BOUND ( 'NONE', #19018, .T. ) ;
#716=VECTOR ( 'NONE', #61353, 1000.000000000000000 ) ;
#717=ORIENTED_EDGE ( 'NONE', *, *, #51275, .F. ) ;
#718=DIRECTION ( 'NONE',  ( -0.7071067811865486830, -0.7071067811865464625, -0.000000000000000000 ) ) ;
#719=LINE ( 'NONE', #121084, #83549 ) ;
#721=PLANE ( 'NONE',  #7126 ) ;
#722=ADVANCED_FACE ( 'NONE', ( #69825 ), #13234, .F. ) ;
#723=ORIENTED_EDGE ( 'NONE', *, *, #4699, .F. ) ;
#724=ADVANCED_FACE ( 'NONE', ( #2348 ), #25555, .F. ) ;
#727=CARTESIAN_POINT ( 'NONE',  ( -33.18398860626899705, 28.73617430169810305, 5.000000000000000000 ) ) ;
#728=CARTESIAN_POINT ( 'NONE',  ( 62.99451991528749772, 28.92564299267982264, 4.000000000000000000 ) ) ;
#729=LINE ( 'NONE', #45023, #17561 ) ;
#731=DIRECTION ( 'NONE',  ( -0.7071067811865487940, 0.7071067811865463515, -0.000000000000000000 ) ) ;
#732=EDGE_LOOP ( 'NONE', ( #19977, #72782, #56165, #112373 ) ) ;
#733=ORIENTED_EDGE ( 'NONE', *, *, #102361, .F. ) ;
#736=EDGE_CURVE ( 'NONE', #98842, #15513, #59650, .T. ) ;
#737=DIRECTION ( 'NONE',  ( 0.7071067811865487940, -0.7071067811865463515, 0.000000000000000000 ) ) ;
#738=VECTOR ( 'NONE', #29742, 999.9999999999998863 ) ;
#739=DIRECTION ( 'NONE',  ( 0.3543493200069162685, -0.000000000000000000, -0.9351131265310288487 ) ) ;
#740=EDGE_CURVE ( 'NONE', #1167, #13678, #45912, .T. ) ;
#741=DIRECTION ( 'NONE',  ( 0.7071067811865486830, -0.7071067811865464625, -0.000000000000000000 ) ) ;
#742=AXIS2_PLACEMENT_3D ( 'NONE', #72568, #104411, #5073 ) ;
#745=VERTEX_POINT ( 'NONE', #106668 ) ;
#746=VECTOR ( 'NONE', #44314, 1000.000000000000000 ) ;
#748=CARTESIAN_POINT ( 'NONE',  ( -10.49999999999992006, 6.052185695429103340, 5.000000000000000000 ) ) ;
#749=EDGE_CURVE ( 'NONE', #77643, #28995, #40049, .T. ) ;
#751=VERTEX_POINT ( 'NONE', #39315 ) ;
#752=EDGE_LOOP ( 'NONE', ( #20197, #50764, #68012, #107527 ) ) ;
#754=ORIENTED_EDGE ( 'NONE', *, *, #126186, .F. ) ;
#755=DIRECTION ( 'NONE',  ( -0.7071067811865486830, -0.7071067811865463515, 0.000000000000000000 ) ) ;
#756=DIRECTION ( 'NONE',  ( -0.3543493200069162685, -0.000000000000000000, -0.9351131265310288487 ) ) ;
#757=CARTESIAN_POINT ( 'NONE',  ( -23.99451991528749062, 28.92564299267954908, 4.000000000000000000 ) ) ;
#758=VECTOR ( 'NONE', #100911, 1000.000000000000227 ) ;
#760=ORIENTED_EDGE ( 'NONE', *, *, #91607, .F. ) ;
#761=ADVANCED_FACE ( 'NONE', ( #6610 ), #61111, .F. ) ;
#765=EDGE_LOOP ( 'NONE', ( #81631, #28554, #45008 ) ) ;
#766=VECTOR ( 'NONE', #69328, 1000.000000000000227 ) ;
#769=CARTESIAN_POINT ( 'NONE',  ( 29.99999999999979039, -10.06887692260770528, 4.000000000000000000 ) ) ;
#771=VERTEX_POINT ( 'NONE', #72696 ) ;
#772=AXIS2_PLACEMENT_3D ( 'NONE', #3609, #81964, #5032 ) ;
#773=PLANE ( 'NONE',  #106202 ) ;
#774=PLANE ( 'NONE',  #135913 ) ;
#775=EDGE_CURVE ( 'NONE', #27298, #47459, #36603, .T. ) ;
#778=FACE_BOUND ( 'NONE', #115100, .T. ) ;
#779=ADVANCED_FACE ( 'NONE', ( #84941 ), #16834, .F. ) ;
#780=ORIENTED_EDGE ( 'NONE', *, *, #73508, .T. ) ;
#781=DIRECTION ( 'NONE',  ( -0.3543493200069162685, -0.000000000000000000, -0.9351131265310288487 ) ) ;
#782=CARTESIAN_POINT ( 'NONE',  ( 28.49999999999979750, -7.912538124160673370, 4.000000000000000000 ) ) ;
#783=LINE ( 'NONE', #90696, #25924 ) ;
#784=LINE ( 'NONE', #11649, #141109 ) ;
#787=CARTESIAN_POINT ( 'NONE',  ( 31.49999999999979039, 16.46639925780209524, 5.000000000000000000 ) ) ;
#788=ORIENTED_EDGE ( 'NONE', *, *, #120399, .T. ) ;
#789=ORIENTED_EDGE ( 'NONE', *, *, #98660, .F. ) ;
#790=ORIENTED_EDGE ( 'NONE', *, *, #83069, .T. ) ;
#791=VECTOR ( 'NONE', #14177, 1000.000000000000000 ) ;
#793=EDGE_CURVE ( 'NONE', #54071, #79781, #96490, .T. ) ;
#794=VECTOR ( 'NONE', #21386, 999.9999999999998863 ) ;
#795=ORIENTED_EDGE ( 'NONE', *, *, #34836, .F. ) ;
#796=EDGE_CURVE ( 'NONE', #61200, #46586, #5914, .T. ) ;
#799=ORIENTED_EDGE ( 'NONE', *, *, #62263, .F. ) ;
#801=CARTESIAN_POINT ( 'NONE',  ( 72.29974487139158157, -27.71228299555256669, 4.000000000000000000 ) ) ;
#803=EDGE_CURVE ( 'NONE', #32716, #98588, #117541, .T. ) ;
#804=DIRECTION ( 'NONE',  ( -0.000000000000000000, 0.000000000000000000, 1.000000000000000000 ) ) ;
#805=CARTESIAN_POINT ( 'NONE',  ( 31.04515773336646944, -21.74070752338406365, 21.72585301388592072 ) ) ;
#807=CARTESIAN_POINT ( 'NONE',  ( -6.489213562373093325, -27.52281430457059841, 5.000000000000000000 ) ) ;
#808=CARTESIAN_POINT ( 'NONE',  ( 25.00193056682080339, -22.22500000000000142, 4.500000000000000888 ) ) ;
#809=ORIENTED_EDGE ( 'NONE', *, *, #143170, .T. ) ;
#810=ORIENTED_EDGE ( 'NONE', *, *, #109263, .F. ) ;
#812=ORIENTED_EDGE ( 'NONE', *, *, #97962, .T. ) ;
#813=ORIENTED_EDGE ( 'NONE', *, *, #115141, .F. ) ;
#814=CARTESIAN_POINT ( 'NONE',  ( 6.328169399223488867, 8.259292476615634371, 4.000000000000000000 ) ) ;
#816=VERTEX_POINT ( 'NONE', #50189 ) ;
#817=ORIENTED_EDGE ( 'NONE', *, *, #106172, .F. ) ;
#819=PLANE ( 'NONE',  #129599 ) ;
#820=VECTOR ( 'NONE', #75844, 1000.000000000000227 ) ;
#822=PLANE ( 'NONE',  #97367 ) ;
#823=EDGE_CURVE ( 'NONE', #46985, #101990, #30576, .T. ) ;
#825=EDGE_CURVE ( 'NONE', #56410, #7821, #8066, .T. ) ;
#828=CARTESIAN_POINT ( 'NONE',  ( 42.18398860626899705, 28.73617430169816700, 5.000000000000000000 ) ) ;
#829=ORIENTED_EDGE ( 'NONE', *, *, #138260, .T. ) ;
#831=DIRECTION ( 'NONE',  ( -0.7071067811865487940, 0.7071067811865463515, -0.000000000000000000 ) ) ;
#833=CARTESIAN_POINT ( 'NONE',  ( 19.05000000000000071, 3.174999999999997158, 5.000000000000000000 ) ) ;
#834=CARTESIAN_POINT ( 'NONE',  ( 28.49999999999979750, -15.29013452822852237, 0.3645803511611025449 ) ) ;
#835=EDGE_LOOP ( 'NONE', ( #4036, #48798, #131663, #1006 ) ) ;
#836=PLANE ( 'NONE',  #18546 ) ;
#837=ORIENTED_EDGE ( 'NONE', *, *, #122262, .F. ) ;
#839=EDGE_CURVE ( 'NONE', #86454, #58696, #17530, .T. ) ;
#840=CARTESIAN_POINT ( 'NONE',  ( -34.44665057663196706, 2.259292476615694323, 14.86850063742362416 ) ) ;
#842=ORIENTED_EDGE ( 'NONE', *, *, #139986, .F. ) ;
#843=DIRECTION ( 'NONE',  ( 0.3543493200069162685, -0.000000000000000000, -0.9351131265310288487 ) ) ;
#844=CARTESIAN_POINT ( 'NONE',  ( -6.938893903907228378E-15, 20.58746187583904330, 4.000000000000000000 ) ) ;
#845=DIRECTION ( 'NONE',  ( 1.000000000000000000, 0.000000000000000000, 0.000000000000000000 ) ) ;
#846=ORIENTED_EDGE ( 'NONE', *, *, #78356, .T. ) ;
#847=CARTESIAN_POINT ( 'NONE',  ( 32.99451991528749062, 28.92564299267960948, 4.000000000000000000 ) ) ;
#848=ORIENTED_EDGE ( 'NONE', *, *, #124268, .F. ) ;
#851=ORIENTED_EDGE ( 'NONE', *, *, #93238, .F. ) ;
#852=ORIENTED_EDGE ( 'NONE', *, *, #6267, .F. ) ;
#854=CARTESIAN_POINT ( 'NONE',  ( -4.499999999999964473, 15.05218569542901896, 5.000000000000000000 ) ) ;
#855=AXIS2_PLACEMENT_3D ( 'NONE', #36138, #25231, #66792 ) ;
#856=EDGE_LOOP ( 'NONE', ( #106789, #129484, #94059, #133606 ) ) ;
#857=CARTESIAN_POINT ( 'NONE',  ( -9.299744871391588674, -27.71228299555212971, 4.000000000000000000 ) ) ;
#861=VERTEX_POINT ( 'NONE', #127749 ) ;
#862=PLANE ( 'NONE',  #42020 ) ;
#866=DIRECTION ( 'NONE',  ( 1.000000000000000000, 0.000000000000000000, 0.000000000000000000 ) ) ;
#868=VECTOR ( 'NONE', #41498, 1000.000000000000000 ) ;
#869=LINE ( 'NONE', #110344, #72055 ) ;
#870=ORIENTED_EDGE ( 'NONE', *, *, #140608, .T. ) ;
#871=VERTEX_POINT ( 'NONE', #73375 ) ;
#872=FACE_OUTER_BOUND ( 'NONE', #17850, .T. ) ;
#873=VECTOR ( 'NONE', #62404, 1000.000000000000000 ) ;
#874=VERTEX_POINT ( 'NONE', #18217 ) ;
#876=DIRECTION ( 'NONE',  ( -0.6830127018922180770, -0.6830127018922204085, -0.2588190451025213501 ) ) ;
#877=DIRECTION ( 'NONE',  ( -0.7071067811865486830, -0.7071067811865464625, 0.000000000000000000 ) ) ;
#879=LINE ( 'NONE', #98087, #27716 ) ;
#880=CARTESIAN_POINT ( 'NONE',  ( -24.64327148205084583, 5.259292476615665457, 4.831541298974430632 ) ) ;
#881=AXIS2_PLACEMENT_3D ( 'NONE', #49592, #61883, #40145 ) ;
#882=EDGE_CURVE ( 'NONE', #47009, #105119, #51619, .T. ) ;
#883=CARTESIAN_POINT ( 'NONE',  ( 11.99451991528749417, 28.92564299267946382, 4.000000000000000000 ) ) ;
#884=( GEOMETRIC_REPRESENTATION_CONTEXT ( 3 ) GLOBAL_UNCERTAINTY_ASSIGNED_CONTEXT ( ( #102893 ) ) GLOBAL_UNIT_ASSIGNED_CONTEXT ( ( #116752, #2986, #47280 ) ) REPRESENTATION_CONTEXT ( 'NONE', 'WORKASPACE' ) );
#885=PLANE ( 'NONE',  #21022 ) ;
#887=EDGE_CURVE ( 'NONE', #116708, #16533, #74072, .T. ) ;
#888=EDGE_LOOP ( 'NONE', ( #37870, #14350, #70171, #3435 ) ) ;
#889=DIRECTION ( 'NONE',  ( 0.3543493200069162685, -0.000000000000000000, -0.9351131265310288487 ) ) ;
#890=DIRECTION ( 'NONE',  ( -0.7071067811865487940, 0.7071067811865463515, -0.000000000000000000 ) ) ;
#891=CARTESIAN_POINT ( 'NONE',  ( 3.328169399223502189, -0.7407075233842770334, 4.000000000000000000 ) ) ;
#893=DIRECTION ( 'NONE',  ( -0.7071067811865486830, -0.7071067811865464625, 0.000000000000000000 ) ) ;
#894=LINE ( 'NONE', #90057, #81597 ) ;
#895=CARTESIAN_POINT ( 'NONE',  ( 29.99999999999979039, 19.55218569542897100, 5.000000000000000000 ) ) ;
#896=AXIS2_PLACEMENT_3D ( 'NONE', #142068, #78228, #86951 ) ;
#897=EDGE_CURVE ( 'NONE', #127404, #117376, #22499, .T. ) ;
#899=EDGE_CURVE ( 'NONE', #138853, #137586, #132029, .T. ) ;
#900=LINE ( 'NONE', #79251, #9697 ) ;
#902=DIRECTION ( 'NONE',  ( -0.6830127018922180770, -0.6830127018922204085, -0.2588190451025213501 ) ) ;
#903=VERTEX_POINT ( 'NONE', #43575 ) ;
#904=ORIENTED_EDGE ( 'NONE', *, *, #70082, .F. ) ;
#906=ADVANCED_FACE ( 'NONE', ( #78353 ), #97204, .F. ) ;
#907=CARTESIAN_POINT ( 'NONE',  ( -4.171830600776438303, 12.75929247661558996, 4.000000000000000000 ) ) ;
#908=VECTOR ( 'NONE', #57091, 1000.000000000000000 ) ;
#909=CARTESIAN_POINT ( 'NONE',  ( -53.99451991528749062, 28.92564299267975869, 4.000000000000000000 ) ) ;
#911=CARTESIAN_POINT ( 'NONE',  ( 24.29974487139158867, -27.71228299555223273, 4.000000000000000000 ) ) ;
#912=LINE ( 'NONE', #136435, #70053 ) ;
#913=EDGE_CURVE ( 'NONE', #62294, #141092, #53006, .T. ) ;
#916=LINE ( 'NONE', #134326, #80419 ) ;
#917=EDGE_LOOP ( 'NONE', ( #64120, #140955, #26192, #20102 ) ) ;
#919=VECTOR ( 'NONE', #125330, 1000.000000000000227 ) ;
#920=DIRECTION ( 'NONE',  ( 0.6830127018922181881, 0.6830127018922202975, -0.2588190451025214056 ) ) ;
#921=EDGE_CURVE ( 'NONE', #50789, #60934, #87792, .T. ) ;
#922=CARTESIAN_POINT ( 'NONE',  ( -19.26506670282039480, 12.75929247661558286, 18.34774599283960939 ) ) ;
#923=LINE ( 'NONE', #188, #18886 ) ;
#924=LINE ( 'NONE', #11071, #53375 ) ;
#925=VERTEX_POINT ( 'NONE', #89230 ) ;
#926=DIRECTION ( 'NONE',  ( 0.7071067811865486830, -0.7071067811865464625, -0.000000000000000000 ) ) ;
#927=VERTEX_POINT ( 'NONE', #10911 ) ;
#928=DIRECTION ( 'NONE',  ( 0.3543493200069162685, -0.000000000000000000, -0.9351131265310288487 ) ) ;
#929=PLANE ( 'NONE',  #64783 ) ;
#931=ADVANCED_FACE ( 'NONE', ( #33454 ), #110230, .F. ) ;
#932=DIRECTION ( 'NONE',  ( -0.7071067811865487940, 0.7071067811865463515, 0.000000000000000000 ) ) ;
#933=CARTESIAN_POINT ( 'NONE',  ( 14.81601139373099585, 28.73617430169776910, 5.000000000000000000 ) ) ;
#934=ORIENTED_EDGE ( 'NONE', *, *, #89062, .F. ) ;
#935=VECTOR ( 'NONE', #129209, 1000.000000000000000 ) ;
#936=CARTESIAN_POINT ( 'NONE',  ( 26.99451991528749417, 28.92564299267956685, 4.000000000000000000 ) ) ;
#940=PLANE ( 'NONE',  #105606 ) ;
#941=LINE ( 'NONE', #78536, #36402 ) ;
#945=ORIENTED_EDGE ( 'NONE', *, *, #128368, .F. ) ;
#947=EDGE_CURVE ( 'NONE', #4808, #99520, #20373, .T. ) ;
#948=CARTESIAN_POINT ( 'NONE',  ( 60.48921356237309510, -27.52281430457097500, 5.000000000000000000 ) ) ;
#949=VERTEX_POINT ( 'NONE', #75501 ) ;
#950=ADVANCED_FACE ( 'NONE', ( #53763 ), #142200, .F. ) ;
#951=CARTESIAN_POINT ( 'NONE',  ( -27.18398860626900060, 28.73617430169806042, 5.000000000000000000 ) ) ;
#952=CARTESIAN_POINT ( 'NONE',  ( -36.33010218547242687, 17.25929247661553845, 19.83885114516079895 ) ) ;
#953=PLANE ( 'NONE',  #143468 ) ;
#954=EDGE_CURVE ( 'NONE', #76142, #77634, #11622, .T. ) ;
#955=DIRECTION ( 'NONE',  ( -0.7071067811865487940, 0.7071067811865463515, -0.000000000000000000 ) ) ;
#956=FACE_BOUND ( 'NONE', #109790, .T. ) ;
#957=CARTESIAN_POINT ( 'NONE',  ( -18.32816939922339472, 17.25929247661555266, 4.000000000000000000 ) ) ;
#958=CARTESIAN_POINT ( 'NONE',  ( -25.49999999999980815, 19.08746187583905041, 4.000000000000000000 ) ) ;
#959=DIRECTION ( 'NONE',  ( 0.7071067811865486830, -0.7071067811865464625, -0.000000000000000000 ) ) ;
#960=LINE ( 'NONE', #45242, #101382 ) ;
#961=CARTESIAN_POINT ( 'NONE',  ( 32.67183060077624646, -9.740707523384177335, 4.000000000000000000 ) ) ;
#962=VERTEX_POINT ( 'NONE', #65363 ) ;
#963=VECTOR ( 'NONE', #101921, 999.9999999999998863 ) ;
#965=ORIENTED_EDGE ( 'NONE', *, *, #26029, .T. ) ;
#967=VERTEX_POINT ( 'NONE', #46478 ) ;
#969=ORIENTED_EDGE ( 'NONE', *, *, #96607, .F. ) ;
#970=EDGE_CURVE ( 'NONE', #139596, #73106, #81223, .T. ) ;
#971=LINE ( 'NONE', #136494, #120723 ) ;
#972=AXIS2_PLACEMENT_3D ( 'NONE', #58558, #82405, #14972 ) ;
#973=ORIENTED_EDGE ( 'NONE', *, *, #18277, .T. ) ;
#974=CARTESIAN_POINT ( 'NONE',  ( 48.48921356237309510, -27.52281430457089328, 5.000000000000000000 ) ) ;
#976=CARTESIAN_POINT ( 'NONE',  ( 30.75860074219774631, 21.72500000000000142, 5.000000000000000000 ) ) ;
#977=DIRECTION ( 'NONE',  ( 0.7071067811865486830, -0.7071067811865464625, -0.000000000000000000 ) ) ;
#978=CARTESIAN_POINT ( 'NONE',  ( -24.58521188482543707, 5.410383847852841654, 4.279600586820024866 ) ) ;
#979=AXIS2_PLACEMENT_3D ( 'NONE', #54919, #23698, #67968 ) ;
#980=PLANE ( 'NONE',  #69093 ) ;
#981=CARTESIAN_POINT ( 'NONE',  ( 25.17183060077629619, -5.240707523384228850, 4.000000000000000000 ) ) ;
#983=CARTESIAN_POINT ( 'NONE',  ( 23.48334561358938899, 22.22500000000000142, 4.500000000000000888 ) ) ;
#984=CARTESIAN_POINT ( 'NONE',  ( -3.793339364578453665, 21.75929247661549581, 4.998822639870701856 ) ) ;
#985=EDGE_LOOP ( 'NONE', ( #90250, #83405, #138439, #103289, #3325 ) ) ;
#986=EDGE_LOOP ( 'NONE', ( #37723, #6916, #143545, #49162 ) ) ;
#987=CARTESIAN_POINT ( 'NONE',  ( 0.000000000000000000, 21.72500000000000142, 4.500000000000000888 ) ) ;
#988=EDGE_LOOP ( 'NONE', ( #94299, #71, #52780 ) ) ;
#989=ORIENTED_EDGE ( 'NONE', *, *, #103086, .T. ) ;
#990=ORIENTED_EDGE ( 'NONE', *, *, #78179, .T. ) ;
#991=AXIS2_PLACEMENT_3D ( 'NONE', #6512, #50791, #39948 ) ;
#993=ORIENTED_EDGE ( 'NONE', *, *, #103380, .F. ) ;
#994=LINE ( 'NONE', #45278, #55610 ) ;
#995=VECTOR ( 'NONE', #112974, 1000.000000000000000 ) ;
#996=ADVANCED_FACE ( 'NONE', ( #67502 ), #80504, .F. ) ;
#997=DIRECTION ( 'NONE',  ( -0.6830127018922181881, 0.6830127018922202975, -0.2588190451025214056 ) ) ;
#999=AXIS2_PLACEMENT_3D ( 'NONE', #25284, #70964, #126056 ) ;
#1000=FACE_OUTER_BOUND ( 'NONE', #61432, .T. ) ;
#1001=EDGE_LOOP ( 'NONE', ( #109061, #123159, #101143, #113750, #111956 ) ) ;
#1002=LINE ( 'NONE', #133691, #29483 ) ;
#1003=DIRECTION ( 'NONE',  ( 0.3543493200069162685, -0.000000000000000000, -0.9351131265310288487 ) ) ;
#1004=LINE ( 'NONE', #111193, #49798 ) ;
#1005=LINE ( 'NONE', #89461, #79703 ) ;
#1006=ORIENTED_EDGE ( 'NONE', *, *, #101122, .T. ) ;
#1007=ORIENTED_EDGE ( 'NONE', *, *, #135968, .F. ) ;
#1008=CARTESIAN_POINT ( 'NONE',  ( 63.18398860626900415, 28.73617430169831621, 5.000000000000000000 ) ) ;
#1010=CYLINDRICAL_SURFACE ( 'NONE', #88540, 0.5000000000000004441 ) ;
#1011=LINE ( 'NONE', #34383, #58711 ) ;
#1012=EDGE_LOOP ( 'NONE', ( #39573, #92186, #49527, #55324 ) ) ;
#1013=VECTOR ( 'NONE', #57020, 1000.000000000000000 ) ;
#1014=DIRECTION ( 'NONE',  ( -0.6830127018922181881, 0.6830127018922202975, -0.2588190451025214056 ) ) ;
#1015=DIRECTION ( 'NONE',  ( -0.000000000000000000, -0.3543493200069152693, 0.9351131265310292928 ) ) ;
#1016=VERTEX_POINT ( 'NONE', #25940 ) ;
#1017=LINE ( 'NONE', #45298, #81912 ) ;
#1019=CARTESIAN_POINT ( 'NONE',  ( -63.48921356237309510, -27.52281430457099631, 5.000000000000000000 ) ) ;
#1020=LINE ( 'NONE', #113357, #141104 ) ;
#1022=CARTESIAN_POINT ( 'NONE',  ( -50.99451991528749062, 28.92564299267973738, 4.000000000000000000 ) ) ;
#1023=DIRECTION ( 'NONE',  ( -0.000000000000000000, -0.3543493200069152693, 0.9351131265310292928 ) ) ;
#1024=LINE ( 'NONE', #33702, #103879 ) ;
#1025=ORIENTED_EDGE ( 'NONE', *, *, #18427, .F. ) ;
#1026=ORIENTED_EDGE ( 'NONE', *, *, #86562, .F. ) ;
#1029=DIRECTION ( 'NONE',  ( 0.3543493200069163240, 0.000000000000000000, 0.9351131265310288487 ) ) ;
#1031=CARTESIAN_POINT ( 'NONE',  ( -20.99999999999985079, 7.007997736742429318, -8.085015511992160953 ) ) ;
#1032=FACE_OUTER_BOUND ( 'NONE', #54625, .T. ) ;
#1033=LINE ( 'NONE', #80087, #118514 ) ;
#1034=ORIENTED_EDGE ( 'NONE', *, *, #129908, .T. ) ;
#1038=LINE ( 'NONE', #56212, #15794 ) ;
#1040=VECTOR ( 'NONE', #97058, 1000.000000000000227 ) ;
#1041=DIRECTION ( 'NONE',  ( 0.3543493200069163240, -0.000000000000000000, 0.9351131265310288487 ) ) ;
#1042=CARTESIAN_POINT ( 'NONE',  ( 3.005480084712505828, 28.92564299267936079, 4.000000000000000000 ) ) ;
#1044=CARTESIAN_POINT ( 'NONE',  ( 19.49999999999987566, -14.94781430457067550, 5.000000000000000000 ) ) ;
#1047=ADVANCED_FACE ( 'NONE', ( #70206 ), #15713, .F. ) ;
#1048=ORIENTED_EDGE ( 'NONE', *, *, #119704, .T. ) ;
#1050=CARTESIAN_POINT ( 'NONE',  ( -54.29974487139159578, -27.71228299555243879, 4.000000000000000000 ) ) ;
#1051=LINE ( 'NONE', #135198, #53564 ) ;
#1052=CARTESIAN_POINT ( 'NONE',  ( 29.99451991528749417, 28.92564299267958816, 4.000000000000000000 ) ) ;
#1053=CARTESIAN_POINT ( 'NONE',  ( 26.29289321881327623, -12.74070752338415247, 5.000000000000000000 ) ) ;
#1054=CARTESIAN_POINT ( 'NONE',  ( -16.26506670282041611, 12.75929247661558996, 18.34774599283960228 ) ) ;
#1055=ADVANCED_FACE ( 'NONE', ( #60005 ), #28802, .F. ) ;
#1056=ADVANCED_FACE ( 'NONE', ( #50539 ), #4109, .F. ) ;
#1057=ORIENTED_EDGE ( 'NONE', *, *, #123182, .T. ) ;
#1058=VERTEX_POINT ( 'NONE', #38245 ) ;
#1059=FACE_OUTER_BOUND ( 'NONE', #79286, .T. ) ;
#1060=PLANE ( 'NONE',  #79155 ) ;
#1063=CARTESIAN_POINT ( 'NONE',  ( 56.99451991528749062, 28.92564299267978001, 4.000000000000000000 ) ) ;
#1064=DIRECTION ( 'NONE',  ( -0.7071067811865486830, -0.7071067811865464625, 0.000000000000000000 ) ) ;
#1065=ADVANCED_FACE ( 'NONE', ( #127376 ), #94729, .F. ) ;
#1067=ADVANCED_FACE ( 'NONE', ( #115751 ), #138990, .F. ) ;
#1069=VECTOR ( 'NONE', #17496, 1000.000000000000000 ) ;
#1070=CARTESIAN_POINT ( 'NONE',  ( 0.000000000000000000, 0.000000000000000000, 5.000000000000000000 ) ) ;
#1071=ORIENTED_EDGE ( 'NONE', *, *, #45808, .T. ) ;
#1073=PLANE ( 'NONE',  #60902 ) ;
#1074=VECTOR ( 'NONE', #110538, 1000.000000000000000 ) ;
#1076=DIRECTION ( 'NONE',  ( -0.6830127018922181881, 0.6830127018922202975, -0.2588190451025214056 ) ) ;
#1077=PLANE ( 'NONE',  #133101 ) ;
#1078=EDGE_CURVE ( 'NONE', #140410, #98076, #28075, .T. ) ;
#1079=ORIENTED_EDGE ( 'NONE', *, *, #104038, .F. ) ;
#1080=FACE_OUTER_BOUND ( 'NONE', #114828, .T. ) ;
#1081=ADVANCED_FACE ( 'NONE', ( #116511 ), #71589, .F. ) ;
#1083=FACE_OUTER_BOUND ( 'NONE', #126972, .T. ) ;
#1085=VERTEX_POINT ( 'NONE', #128116 ) ;
#1086=VERTEX_POINT ( 'NONE', #17198 ) ;
#1087=DIRECTION ( 'NONE',  ( 0.6830127018922180770, -0.6830127018922204085, -0.2588190451025213501 ) ) ;
#1088=CARTESIAN_POINT ( 'NONE',  ( 41.99451991528749062, 28.92564299267967343, 4.000000000000000000 ) ) ;
#1089=EDGE_CURVE ( 'NONE', #138081, #131497, #61458, .T. ) ;
#1092=PLANE ( 'NONE',  #99515 ) ;
#1093=CARTESIAN_POINT ( 'NONE',  ( 34.49999999999975842, -2.945670655169024155, 4.994342998332159667 ) ) ;
#1097=DIRECTION ( 'NONE',  ( -0.3543493200069163240, -0.000000000000000000, 0.9351131265310288487 ) ) ;
#1099=DIRECTION ( 'NONE',  ( 1.000000000000000000, 0.000000000000000000, 0.000000000000000000 ) ) ;
#1100=ORIENTED_EDGE ( 'NONE', *, *, #136821, .F. ) ;
#1102=ORIENTED_EDGE ( 'NONE', *, *, #130845, .F. ) ;
#1105=ORIENTED_EDGE ( 'NONE', *, *, #121183, .T. ) ;
#1106=AXIS2_PLACEMENT_3D ( 'NONE', #54858, #8428, #9135 ) ;
#1107=DIRECTION ( 'NONE',  ( -0.7071067811865486830, -0.7071067811865464625, -0.000000000000000000 ) ) ;
#1109=DIRECTION ( 'NONE',  ( -0.000000000000000000, -0.000000000000000000, 1.000000000000000000 ) ) ;
#1110=EDGE_CURVE ( 'NONE', #9952, #4761, #29480, .T. ) ;
#1111=LINE ( 'NONE', #12710, #57346 ) ;
#1112=DIRECTION ( 'NONE',  ( -0.7071067811865486830, -0.7071067811865464625, 0.000000000000000000 ) ) ;
#1113=EDGE_LOOP ( 'NONE', ( #101021, #24489, #97914, #30059 ) ) ;
#1114=ORIENTED_EDGE ( 'NONE', *, *, #50311, .F. ) ;
#1115=CARTESIAN_POINT ( 'NONE',  ( -63.29974487139158867, -27.71228299555250274, 4.000000000000000000 ) ) ;
#1117=ADVANCED_FACE ( 'NONE', ( #106305 ), #51266, .F. ) ;
#1118=ORIENTED_EDGE ( 'NONE', *, *, #19224, .F. ) ;
#1120=EDGE_CURVE ( 'NONE', #69887, #22434, #79304, .T. ) ;
#1121=LINE ( 'NONE', #45399, #73463 ) ;
#1122=DIRECTION ( 'NONE',  ( -0.7071067811865487940, 0.7071067811865463515, -0.000000000000000000 ) ) ;
#1123=ADVANCED_FACE ( 'NONE', ( #22000 ), #44524, .T. ) ;
#1124=ORIENTED_EDGE ( 'NONE', *, *, #37881, .T. ) ;
#1125=ADVANCED_FACE ( 'NONE', ( #66956 ), #107052, .F. ) ;
#1126=FACE_BOUND ( 'NONE', #89379, .T. ) ;
#1127=LINE ( 'NONE', #2551, #131276 ) ;
#1128=LINE ( 'NONE', #134546, #37408 ) ;
#1130=DIRECTION ( 'NONE',  ( -0.6830127018922181881, 0.6830127018922202975, -0.2588190451025214056 ) ) ;
#1131=CARTESIAN_POINT ( 'NONE',  ( -34.82816939922327748, 9.759292476615621936, 4.000000000000000000 ) ) ;
#1133=ORIENTED_EDGE ( 'NONE', *, *, #19224, .T. ) ;
#1134=ORIENTED_EDGE ( 'NONE', *, *, #138991, .T. ) ;
#1136=ORIENTED_EDGE ( 'NONE', *, *, #74828, .F. ) ;
#1137=EDGE_CURVE ( 'NONE', #131909, #97989, #100301, .T. ) ;
#1138=DIRECTION ( 'NONE',  ( -0.000000000000000000, 0.000000000000000000, 1.000000000000000000 ) ) ;
#1139=EDGE_LOOP ( 'NONE', ( #35677, #126554, #84697, #96997 ) ) ;
#1140=DIRECTION ( 'NONE',  ( -0.7071067811865486830, 0.7071067811865464625, 0.000000000000000000 ) ) ;
#1142=CARTESIAN_POINT ( 'NONE',  ( 5.994519915287488843, 28.92564299267942118, 4.000000000000000000 ) ) ;
#1143=ORIENTED_EDGE ( 'NONE', *, *, #103846, .T. ) ;
#1144=CARTESIAN_POINT ( 'NONE',  ( -10.49999999999991829, 19.46639925780206326, 5.000000000000000000 ) ) ;
#1145=CARTESIAN_POINT ( 'NONE',  ( 59.99451991528749772, 28.92564299267980132, 4.000000000000000000 ) ) ;
#1146=PLANE ( 'NONE',  #66295 ) ;
#1147=CARTESIAN_POINT ( 'NONE',  ( 18.18398860626898994, 28.73617430169800002, 5.000000000000000000 ) ) ;
#1148=CARTESIAN_POINT ( 'NONE',  ( -24.18398860626899705, 28.73617430169804265, 5.000000000000000000 ) ) ;
#1149=CARTESIAN_POINT ( 'NONE',  ( 34.42499999999998295, 22.22500000000000142, 5.000000000000000000 ) ) ;
#1151=ORIENTED_EDGE ( 'NONE', *, *, #3377, .T. ) ;
#1153=CARTESIAN_POINT ( 'NONE',  ( 50.99451991528749062, 28.92564299267973738, 4.000000000000000000 ) ) ;
#1155=ADVANCED_FACE ( 'NONE', ( #51979 ), #953, .F. ) ;
#1156=VERTEX_POINT ( 'NONE', #67705 ) ;
#1157=ORIENTED_EDGE ( 'NONE', *, *, #68554, .T. ) ;
#1159=ORIENTED_EDGE ( 'NONE', *, *, #141206, .T. ) ;
#1160=LINE ( 'NONE', #21523, #62927 ) ;
#1161=VECTOR ( 'NONE', #121622, 1000.000000000000000 ) ;
#1162=EDGE_CURVE ( 'NONE', #123801, #89060, #111889, .T. ) ;
#1165=LINE ( 'NONE', #67173, #84196 ) ;
#1166=EDGE_CURVE ( 'NONE', #128760, #71811, #56834, .T. ) ;
#1167=VERTEX_POINT ( 'NONE', #45930 ) ;
#1168=AXIS2_PLACEMENT_3D ( 'NONE', #40012, #29099, #31776 ) ;
#1169=EDGE_CURVE ( 'NONE', #56720, #4770, #80696, .T. ) ;
#1170=DIRECTION ( 'NONE',  ( -0.3543493200069162685, -0.000000000000000000, -0.9351131265310288487 ) ) ;
#1171=ORIENTED_EDGE ( 'NONE', *, *, #136792, .F. ) ;
#1172=DIRECTION ( 'NONE',  ( -0.6830127018922180770, -0.6830127018922204085, -0.2588190451025213501 ) ) ;
#1173=CARTESIAN_POINT ( 'NONE',  ( -11.81601139373100651, 28.73617430169779041, 5.000000000000000000 ) ) ;
#1174=VERTEX_POINT ( 'NONE', #69107 ) ;
#1175=EDGE_CURVE ( 'NONE', #104818, #11807, #13965, .T. ) ;
#1176=DIRECTION ( 'NONE',  ( 0.000000000000000000, 0.000000000000000000, 1.000000000000000000 ) ) ;
#1177=CARTESIAN_POINT ( 'NONE',  ( 2.510786437626908008, -27.52281430457053446, 5.000000000000000000 ) ) ;
#1178=ORIENTED_EDGE ( 'NONE', *, *, #48064, .F. ) ;
#1181=VECTOR ( 'NONE', #15133, 1000.000000000000000 ) ;
#1182=EDGE_LOOP ( 'NONE', ( #123591, #125967, #138779, #93583 ) ) ;
#1183=EDGE_LOOP ( 'NONE', ( #4775, #85337, #276, #105897 ) ) ;
#1185=LINE ( 'NONE', #67947, #137352 ) ;
#1186=CARTESIAN_POINT ( 'NONE',  ( 14.20710678118645376, 12.75929247661558996, 5.000000000000000000 ) ) ;
#1188=EDGE_CURVE ( 'NONE', #127957, #23069, #90867, .T. ) ;
#1189=LINE ( 'NONE', #89649, #25674 ) ;
#1190=VERTEX_POINT ( 'NONE', #57524 ) ;
#1191=DIRECTION ( 'NONE',  ( 0.6830127018922181881, 0.6830127018922202975, -0.2588190451025214056 ) ) ;
#1192=VECTOR ( 'NONE', #13568, 1000.000000000000000 ) ;
#1193=AXIS2_PLACEMENT_3D ( 'NONE', #10456, #9746, #32235 ) ;
#1195=LINE ( 'NONE', #101964, #87911 ) ;
#1196=AXIS2_PLACEMENT_3D ( 'NONE', #52105, #133091, #33772 ) ;
#1197=CARTESIAN_POINT ( 'NONE',  ( -32.00492477221175136, -5.240707523384228850, 12.38332538355503409 ) ) ;
#1198=VECTOR ( 'NONE', #26699, 1000.000000000000000 ) ;
#1199=CARTESIAN_POINT ( 'NONE',  ( -39.48921356237310221, -27.52281430457082934, 5.000000000000000000 ) ) ;
#1200=ORIENTED_EDGE ( 'NONE', *, *, #8875, .T. ) ;
#1201=ORIENTED_EDGE ( 'NONE', *, *, #73588, .T. ) ;
#1202=ORIENTED_EDGE ( 'NONE', *, *, #5532, .T. ) ;
#1204=CARTESIAN_POINT ( 'NONE',  ( 28.17183060077628198, -2.240707523384254163, 4.000000000000000000 ) ) ;
#1206=LINE ( 'NONE', #98413, #61291 ) ;
#1207=FACE_OUTER_BOUND ( 'NONE', #10102, .T. ) ;
#1209=CARTESIAN_POINT ( 'NONE',  ( -57.18398860626899705, 28.73617430169827358, 5.000000000000000000 ) ) ;
#1210=CARTESIAN_POINT ( 'NONE',  ( -7.499999999999940492, -1.912538124160739095, 4.000000000000000000 ) ) ;
#1211=DIRECTION ( 'NONE',  ( 0.7071067811865486830, -0.7071067811865464625, -0.000000000000000000 ) ) ;
#1212=DIRECTION ( 'NONE',  ( -0.6830127018922181881, 0.6830127018922202975, -0.2588190451025214056 ) ) ;
#1213=VERTEX_POINT ( 'NONE', #101711 ) ;
#1215=EDGE_LOOP ( 'NONE', ( #133131, #72921, #116682, #12853 ) ) ;
#1217=ORIENTED_EDGE ( 'NONE', *, *, #127215, .T. ) ;
#1218=LINE ( 'NONE', #1910, #117720 ) ;
#1219=CARTESIAN_POINT ( 'NONE',  ( 7.499999999999949374, 6.052185695429103340, 5.000000000000000000 ) ) ;
#1220=ORIENTED_EDGE ( 'NONE', *, *, #119260, .F. ) ;
#1222=DIRECTION ( 'NONE',  ( 0.6830127018922180770, -0.6830127018922204085, -0.2588190451025213501 ) ) ;
#1224=EDGE_LOOP ( 'NONE', ( #85581, #115658, #42988, #56556 ) ) ;
#1225=CARTESIAN_POINT ( 'NONE',  ( -72.18398860626899705, 28.73617430169837661, 5.000000000000000000 ) ) ;
#1226=ORIENTED_EDGE ( 'NONE', *, *, #75166, .F. ) ;
#1230=CARTESIAN_POINT ( 'NONE',  ( -5.292893218813416567, 8.259292476615632594, 5.000000000000000000 ) ) ;
#1232=EDGE_CURVE ( 'NONE', #106471, #108854, #48777, .T. ) ;
#1233=LINE ( 'NONE', #78845, #27718 ) ;
#1234=ORIENTED_EDGE ( 'NONE', *, *, #47549, .T. ) ;
#1235=EDGE_CURVE ( 'NONE', #89696, #57963, #115397, .T. ) ;
#1237=LINE ( 'NONE', #66535, #7897 ) ;
#1238=EDGE_CURVE ( 'NONE', #142920, #91253, #19690, .T. ) ;
#1239=DIRECTION ( 'NONE',  ( 0.6830127018922180770, -0.6830127018922204085, -0.2588190451025213501 ) ) ;
#1241=LINE ( 'NONE', #102737, #56051 ) ;
#1242=CARTESIAN_POINT ( 'NONE',  ( 65.99451991528749772, 28.92564299267984396, 4.000000000000000000 ) ) ;
#1243=CARTESIAN_POINT ( 'NONE',  ( 29.20710678118634007, -8.240707523384203981, 5.000000000000000000 ) ) ;
#1244=EDGE_CURVE ( 'NONE', #24821, #66605, #107417, .T. ) ;
#1245=VERTEX_POINT ( 'NONE', #5930 ) ;
#1246=EDGE_LOOP ( 'NONE', ( #48610, #109261, #97300, #61995 ) ) ;
#1248=EDGE_CURVE ( 'NONE', #52184, #99523, #50206, .T. ) ;
#1250=EDGE_CURVE ( 'NONE', #59483, #94981, #53019, .T. ) ;
#1252=CARTESIAN_POINT ( 'NONE',  ( -8.531356016368066619, 22.22500000000000142, 15.00153835162133475 ) ) ;
#1254=DIRECTION ( 'NONE',  ( -0.000000000000000000, -0.3543493200069152693, 0.9351131265310292928 ) ) ;
#1255=ORIENTED_EDGE ( 'NONE', *, *, #118819, .F. ) ;
#1256=PLANE ( 'NONE',  #10391 ) ;
#1257=CARTESIAN_POINT ( 'NONE',  ( -6.316579611327855837, -6.740707523384212863, 11.88629033278125746 ) ) ;
#1258=ADVANCED_FACE ( 'NONE', ( #7373 ), #95826, .F. ) ;
#1259=LINE ( 'NONE', #102031, #106730 ) ;
#1260=EDGE_CURVE ( 'NONE', #50292, #107270, #121139, .T. ) ;
#1261=LINE ( 'NONE', #45545, #141113 ) ;
#1263=DIRECTION ( 'NONE',  ( 0.6830127018922181881, 0.6830127018922202975, -0.2588190451025214056 ) ) ;
#1264=ORIENTED_EDGE ( 'NONE', *, *, #33892, .F. ) ;
#1266=DIRECTION ( 'NONE',  ( -0.7071067811865487940, 0.7071067811865463515, -0.000000000000000000 ) ) ;
#1267=DIRECTION ( 'NONE',  ( -0.7071067811865486830, -0.7071067811865464625, -0.000000000000000000 ) ) ;
#1272=VECTOR ( 'NONE', #142529, 999.9999999999998863 ) ;
#1273=ORIENTED_EDGE ( 'NONE', *, *, #42125, .T. ) ;
#1274=VERTEX_POINT ( 'NONE', #76228 ) ;
#1276=ORIENTED_EDGE ( 'NONE', *, *, #52310, .T. ) ;
#1277=VECTOR ( 'NONE', #51961, 1000.000000000000227 ) ;
#1278=CARTESIAN_POINT ( 'NONE',  ( 32.99999999999977973, -6.412538124160687580, 4.000000000000000000 ) ) ;
#1279=CARTESIAN_POINT ( 'NONE',  ( 14.97558742549547794, -1.187250289053316088, 4.247958624336164668 ) ) ;
#1280=DIRECTION ( 'NONE',  ( 0.7071067811865487940, -0.7071067811865463515, 0.000000000000000000 ) ) ;
#1281=LINE ( 'NONE', #13581, #24591 ) ;
#1283=DIRECTION ( 'NONE',  ( -0.7071067811865486830, -0.7071067811865464625, 0.000000000000000000 ) ) ;
#1285=( BOUNDED_CURVE ( )  B_SPLINE_CURVE ( 3, ( #10003, #133935, #89708, #110022 ),
 .UNSPECIFIED., .F., .F. ) 
 B_SPLINE_CURVE_WITH_KNOTS ( ( 4, 4 ),
 ( 5.106027341939277875, 6.645403452391244414 ),
 .UNSPECIFIED. ) 
 CURVE ( )  GEOMETRIC_REPRESENTATION_ITEM ( )  RATIONAL_B_SPLINE_CURVE ( ( 1.000000000000000000, 0.8120851936182275077, 0.8120851936182275077, 1.000000000000000000 ) ) 
 REPRESENTATION_ITEM ( '' )  );
#1286=CARTESIAN_POINT ( 'NONE',  ( 57.29974487139158157, -27.71228299555246011, 4.000000000000000000 ) ) ;
#1288=VECTOR ( 'NONE', #116450, 1000.000000000000000 ) ;
#1289=ORIENTED_EDGE ( 'NONE', *, *, #44710, .F. ) ;
#1290=DIRECTION ( 'NONE',  ( 0.7071067811865487940, 0.7071067811865463515, 0.000000000000000000 ) ) ;
#1291=EDGE_CURVE ( 'NONE', #86454, #32049, #43589, .T. ) ;
#1292=CARTESIAN_POINT ( 'NONE',  ( 27.48921356237309155, -27.52281430457074762, 5.000000000000000000 ) ) ;
#1293=ORIENTED_EDGE ( 'NONE', *, *, #77447, .F. ) ;
#1295=LINE ( 'NONE', #14338, #102420 ) ;
#1296=LINE ( 'NONE', #12894, #36184 ) ;
#1298=LINE ( 'NONE', #36117, #81309 ) ;
#1299=DIRECTION ( 'NONE',  ( 0.7071067811865487940, 0.7071067811865463515, -0.000000000000000000 ) ) ;
#1300=EDGE_CURVE ( 'NONE', #106183, #141363, #142217, .T. ) ;
#1302=CARTESIAN_POINT ( 'NONE',  ( -33.18398860626899705, 28.73617430169810305, 5.000000000000000000 ) ) ;
#1305=VECTOR ( 'NONE', #138783, 1000.000000000000114 ) ;
#1307=AXIS2_PLACEMENT_3D ( 'NONE', #122764, #67720, #32944 ) ;
#1309=LINE ( 'NONE', #85131, #64250 ) ;
#1310=ADVANCED_FACE ( 'NONE', ( #132047 ), #119686, .F. ) ;
#1311=VERTEX_POINT ( 'NONE', #20387 ) ;
#1313=AXIS2_PLACEMENT_3D ( 'NONE', #138192, #72269, #83097 ) ;
#1315=VERTEX_POINT ( 'NONE', #76971 ) ;
#1317=DIRECTION ( 'NONE',  ( -0.3543493200069162685, -0.000000000000000000, -0.9351131265310288487 ) ) ;
#1318=ADVANCED_FACE ( 'NONE', ( #130632 ), #75517, .F. ) ;
#1319=CARTESIAN_POINT ( 'NONE',  ( 0.000000000000000000, 0.000000000000000000, 5.000000000000000000 ) ) ;
#1320=DIRECTION ( 'NONE',  ( 0.7071067811865487940, 0.7071067811865463515, 0.000000000000000000 ) ) ;
#1321=ORIENTED_EDGE ( 'NONE', *, *, #26511, .T. ) ;
#1323=ORIENTED_EDGE ( 'NONE', *, *, #90940, .F. ) ;
#1324=DIRECTION ( 'NONE',  ( 0.6830127018922181881, 0.6830127018922202975, -0.2588190451025214056 ) ) ;
#1325=ADVANCED_FACE ( 'NONE', ( #66780 ), #774, .T. ) ;
#1326=EDGE_LOOP ( 'NONE', ( #260, #7384, #48856, #127940 ) ) ;
#1328=ORIENTED_EDGE ( 'NONE', *, *, #99413, .F. ) ;
#1329=PLANE ( 'NONE',  #140790 ) ;
#1330=ORIENTED_EDGE ( 'NONE', *, *, #53151, .T. ) ;
#1331=ORIENTED_EDGE ( 'NONE', *, *, #70841, .T. ) ;
#1333=FACE_OUTER_BOUND ( 'NONE', #102147, .T. ) ;
#1334=CARTESIAN_POINT ( 'NONE',  ( -8.700255128608413102, -27.71228299555199825, 4.000000000000000000 ) ) ;
#1336=LINE ( 'NONE', #112283, #107401 ) ;
#1339=DIRECTION ( 'NONE',  ( 0.7071067811865487940, 0.7071067811865463515, 0.000000000000000000 ) ) ;
#1340=CARTESIAN_POINT ( 'NONE',  ( 15.48921356237309510, -27.52281430457066236, 5.000000000000000000 ) ) ;
#1341=CARTESIAN_POINT ( 'NONE',  ( -9.722814304570524868, -21.72500000000000497, 5.000000000000000000 ) ) ;
#1343=VERTEX_POINT ( 'NONE', #45069 ) ;
#1344=EDGE_CURVE ( 'NONE', #48060, #114516, #12378, .T. ) ;
#1345=CARTESIAN_POINT ( 'NONE',  ( 17.57538274164440040, -2.608983483842240325, 5.000000000000000000 ) ) ;
#1346=DIRECTION ( 'NONE',  ( 0.7071067811865487940, 0.7071067811865463515, 0.000000000000000000 ) ) ;
#1347=DIRECTION ( 'NONE',  ( -0.7071067811865486830, -0.7071067811865464625, 0.000000000000000000 ) ) ;
#1348=EDGE_LOOP ( 'NONE', ( #40969, #4224, #128380, #788, #67686, #50092, #101673, #38774, #62214, #112247, #107375, #138463, #133997, #65653, #92971, #39749, #60305, #21777, #3018, #81975, #44225, #99062, #121351, #87831, #27165, #142601, #12354, #79618, #22556, #95417, #98165, #72518, #24293, #107396, #1773, #20521, #129040, #59526 ) ) ;
#1349=VERTEX_POINT ( 'NONE', #11640 ) ;
#1350=DIRECTION ( 'NONE',  ( -0.6830127018922181881, 0.6830127018922202975, -0.2588190451025214056 ) ) ;
#1351=ORIENTED_EDGE ( 'NONE', *, *, #98474, .F. ) ;
#1353=CARTESIAN_POINT ( 'NONE',  ( 57.29974487139158157, -27.71228299555246011, 4.000000000000000000 ) ) ;
#1355=CARTESIAN_POINT ( 'NONE',  ( -1.637538124160967001, 22.22500000000000142, 4.000000000000000000 ) ) ;
#1356=EDGE_CURVE ( 'NONE', #76633, #89639, #55919, .T. ) ;
#1359=PLANE ( 'NONE',  #139009 ) ;
#1360=EDGE_LOOP ( 'NONE', ( #126214, #64444, #65547, #24000 ) ) ;
#1362=VECTOR ( 'NONE', #6419, 1000.000000000000000 ) ;
#1366=CARTESIAN_POINT ( 'NONE',  ( 31.49999999999977973, -11.56887692260769285, 4.000000000000000000 ) ) ;
#1367=AXIS2_PLACEMENT_3D ( 'NONE', #27872, #61279, #19142 ) ;
#1368=DIRECTION ( 'NONE',  ( 0.7071067811865487940, 0.7071067811865463515, 0.000000000000000000 ) ) ;
#1370=VERTEX_POINT ( 'NONE', #34156 ) ;
#1371=ORIENTED_EDGE ( 'NONE', *, *, #53949, .F. ) ;
#1372=LINE ( 'NONE', #95894, #109803 ) ;
#1374=FACE_OUTER_BOUND ( 'NONE', #130641, .T. ) ;
#1375=DIRECTION ( 'NONE',  ( 0.7071067811865487940, -0.7071067811865463515, 0.000000000000000000 ) ) ;
#1376=EDGE_CURVE ( 'NONE', #85512, #4593, #1479, .T. ) ;
#1377=ORIENTED_EDGE ( 'NONE', *, *, #98353, .T. ) ;
#1378=CARTESIAN_POINT ( 'NONE',  ( -34.42500000000001137, -21.72500000000000142, 4.500000000000000888 ) ) ;
#1379=VECTOR ( 'NONE', #78654, 999.9999999999998863 ) ;
#1380=DIRECTION ( 'NONE',  ( -0.7071067811865486830, -0.7071067811865464625, 0.000000000000000000 ) ) ;
#1383=CARTESIAN_POINT ( 'NONE',  ( -19.05000000000000071, 3.174999999999997158, 5.000000000000000000 ) ) ;
#1384=CARTESIAN_POINT ( 'NONE',  ( 34.42499999999998295, 0.000000000000000000, 4.500000000000000888 ) ) ;
#1385=ORIENTED_EDGE ( 'NONE', *, *, #44170, .T. ) ;
#1388=ORIENTED_EDGE ( 'NONE', *, *, #111799, .T. ) ;
#1389=CARTESIAN_POINT ( 'NONE',  ( 34.92499999999998295, -7.487538124160447950, 4.000000000000000000 ) ) ;
#1391=ORIENTED_EDGE ( 'NONE', *, *, #140476, .F. ) ;
#1394=AXIS2_PLACEMENT_3D ( 'NONE', #92961, #114694, #58248 ) ;
#1395=CARTESIAN_POINT ( 'NONE',  ( -32.20710678118631876, -2.240707523384264377, 5.000000000000000000 ) ) ;
#1396=LINE ( 'NONE', #81149, #117940 ) ;
#1397=AXIS2_PLACEMENT_3D ( 'NONE', #38406, #114520, #71053 ) ;
#1398=EDGE_CURVE ( 'NONE', #6574, #114790, #31302, .T. ) ;
#1399=CARTESIAN_POINT ( 'NONE',  ( 27.18398860626900060, 28.73617430169806042, 5.000000000000000000 ) ) ;
#1400=LINE ( 'NONE', #113761, #82996 ) ;
#1401=EDGE_CURVE ( 'NONE', #91522, #20875, #13079, .T. ) ;
#1402=DIRECTION ( 'NONE',  ( -0.7071067811865486830, 0.7071067811865464625, 0.000000000000000000 ) ) ;
#1403=CARTESIAN_POINT ( 'NONE',  ( 0.7928932188134476533, -2.240707523384262601, 5.000000000000000000 ) ) ;
#1404=CARTESIAN_POINT ( 'NONE',  ( 39.48921356237310221, -27.52281430457082934, 5.000000000000000000 ) ) ;
#1405=ADVANCED_FACE ( 'NONE', ( #114545 ), #136301, .F. ) ;
#1406=DIRECTION ( 'NONE',  ( -0.3543493200069162685, -0.000000000000000000, -0.9351131265310288487 ) ) ;
#1409=PLANE ( 'NONE',  #92278 ) ;
#1410=VECTOR ( 'NONE', #48517, 1000.000000000000000 ) ;
#1412=CARTESIAN_POINT ( 'NONE',  ( 0.000000000000000000, 0.000000000000000000, 5.000000000000000000 ) ) ;
#1413=EDGE_CURVE ( 'NONE', #39017, #37842, #16246, .T. ) ;
#1414=VERTEX_POINT ( 'NONE', #92074 ) ;
#1417=EDGE_LOOP ( 'NONE', ( #107064, #64039, #40241, #73848 ) ) ;
#1418=VERTEX_POINT ( 'NONE', #124719 ) ;
#1419=ORIENTED_EDGE ( 'NONE', *, *, #126471, .F. ) ;
#1420=CARTESIAN_POINT ( 'NONE',  ( -20.99999999999985789, -16.44781430457065952, 5.000000000000000000 ) ) ;
#1422=ORIENTED_EDGE ( 'NONE', *, *, #49308, .T. ) ;
#1424=CARTESIAN_POINT ( 'NONE',  ( 18.18398860626898994, 28.73617430169800002, 5.000000000000000000 ) ) ;
#1425=ADVANCED_FACE ( 'NONE', ( #123322 ), #115223, .F. ) ;
#1427=CARTESIAN_POINT ( 'NONE',  ( 5.510786437626906675, -27.52281430457051314, 5.000000000000000000 ) ) ;
#1428=EDGE_LOOP ( 'NONE', ( #35076, #122709, #134803, #121004 ) ) ;
#1431=DIRECTION ( 'NONE',  ( -0.7071067811865487940, 0.7071067811865463515, 0.000000000000000000 ) ) ;
#1432=LINE ( 'NONE', #55142, #137712 ) ;
#1433=CARTESIAN_POINT ( 'NONE',  ( 34.49999999999975842, 15.05432934483078888, 4.994342998332163219 ) ) ;
#1434=LINE ( 'NONE', #102930, #31347 ) ;
#1436=CARTESIAN_POINT ( 'NONE',  ( 34.42499999999998295, -7.458600742197882383, 5.000000000000000000 ) ) ;
#1438=EDGE_CURVE ( 'NONE', #81104, #49860, #2180, .T. ) ;
#1439=CARTESIAN_POINT ( 'NONE',  ( 34.92499999999998295, 7.067865804795108176, 10.74360474999299342 ) ) ;
#1440=ORIENTED_EDGE ( 'NONE', *, *, #89087, .F. ) ;
#1441=VERTEX_POINT ( 'NONE', #95646 ) ;
#1443=( BOUNDED_CURVE ( )  B_SPLINE_CURVE ( 3, ( #73077, #117229, #93369, #106347 ),
 .UNSPECIFIED., .F., .T. ) 
 B_SPLINE_CURVE_WITH_KNOTS ( ( 4, 4 ),
 ( 1.964434688349483871, 3.503810798801452187 ),
 .UNSPECIFIED. ) 
 CURVE ( )  GEOMETRIC_REPRESENTATION_ITEM ( )  RATIONAL_B_SPLINE_CURVE ( ( 1.000000000000000000, 0.8120851936182270636, 0.8120851936182270636, 1.000000000000000000 ) ) 
 REPRESENTATION_ITEM ( '' )  );
#1444=ORIENTED_EDGE ( 'NONE', *, *, #135572, .F. ) ;
#1445=CARTESIAN_POINT ( 'NONE',  ( -2.999999999999981792, 4.931123077392134846, 4.000000000000000000 ) ) ;
#1446=ADVANCED_FACE ( 'NONE', ( #40583 ), #127578, .T. ) ;
#1448=DIRECTION ( 'NONE',  ( 0.7071067811865487940, 0.7071067811865463515, -0.000000000000000000 ) ) ;
#1450=PLANE ( 'NONE',  #127662 ) ;
#1452=ORIENTED_EDGE ( 'NONE', *, *, #25871, .T. ) ;
#1453=VERTEX_POINT ( 'NONE', #115958 ) ;
#1455=VECTOR ( 'NONE', #16197, 1000.000000000000000 ) ;
#1456=DIRECTION ( 'NONE',  ( 0.7071067811865487940, 0.7071067811865463515, -0.000000000000000000 ) ) ;
#1457=EDGE_LOOP ( 'NONE', ( #117782, #72152, #105613, #133932 ) ) ;
#1458=ORIENTED_EDGE ( 'NONE', *, *, #52172, .F. ) ;
#1461=LINE ( 'NONE', #6429, #42184 ) ;
#1463=( BOUNDED_CURVE ( )  B_SPLINE_CURVE ( 3, ( #123074, #133940, #90430, #546 ),
 .UNSPECIFIED., .F., .T. ) 
 B_SPLINE_CURVE_WITH_KNOTS ( ( 4, 4 ),
 ( 5.920967161967927161, 7.341195215986644484 ),
 .UNSPECIFIED. ) 
 CURVE ( )  GEOMETRIC_REPRESENTATION_ITEM ( )  RATIONAL_B_SPLINE_CURVE ( ( 1.000000000000000000, 0.8388583629366599403, 0.8388583629366599403, 1.000000000000000000 ) ) 
 REPRESENTATION_ITEM ( '' )  );
#1464=EDGE_CURVE ( 'NONE', #114304, #124605, #49338, .T. ) ;
#1465=VECTOR ( 'NONE', #113483, 1000.000000000000000 ) ;
#1466=LINE ( 'NONE', #79103, #133371 ) ;
#1467=VERTEX_POINT ( 'NONE', #116695 ) ;
#1468=VECTOR ( 'NONE', #7725, 1000.000000000000227 ) ;
#1469=FACE_OUTER_BOUND ( 'NONE', #87679, .T. ) ;
#1470=ORIENTED_EDGE ( 'NONE', *, *, #91967, .T. ) ;
#1471=ORIENTED_EDGE ( 'NONE', *, *, #26179, .F. ) ;
#1472=VERTEX_POINT ( 'NONE', #84783 ) ;
#1473=DIRECTION ( 'NONE',  ( 0.6830127018922181881, 0.6830127018922202975, -0.2588190451025214056 ) ) ;
#1474=CARTESIAN_POINT ( 'NONE',  ( 29.99999999999979039, 1.931123077392167264, 4.000000000000000000 ) ) ;
#1475=ORIENTED_EDGE ( 'NONE', *, *, #5643, .F. ) ;
#1476=DIRECTION ( 'NONE',  ( 0.6830127018922180770, -0.6830127018922204085, -0.2588190451025213501 ) ) ;
#1478=EDGE_CURVE ( 'NONE', #60822, #110777, #93522, .T. ) ;
#1479=LINE ( 'NONE', #111709, #50245 ) ;
#1481=CARTESIAN_POINT ( 'NONE',  ( -75.29974487139158157, -27.71228299555258445, 4.000000000000000000 ) ) ;
#1483=FACE_BOUND ( 'NONE', #94642, .T. ) ;
#1485=DIRECTION ( 'NONE',  ( 0.3543493200069162685, -0.000000000000000000, -0.9351131265310288487 ) ) ;
#1487=EDGE_CURVE ( 'NONE', #89682, #91342, #71787, .T. ) ;
#1488=DIRECTION ( 'NONE',  ( 0.6830127018922180770, -0.6830127018922204085, -0.2588190451025213501 ) ) ;
#1489=FACE_OUTER_BOUND ( 'NONE', #13573, .T. ) ;
#1490=VERTEX_POINT ( 'NONE', #96331 ) ;
#1491=DIRECTION ( 'NONE',  ( -0.7071067811865486830, 0.7071067811865464625, 0.000000000000000000 ) ) ;
#1492=EDGE_LOOP ( 'NONE', ( #55613, #119762, #135155, #110848 ) ) ;
#1493=ORIENTED_EDGE ( 'NONE', *, *, #59045, .F. ) ;
#1495=ORIENTED_EDGE ( 'NONE', *, *, #87274, .F. ) ;
#1496=VECTOR ( 'NONE', #118446, 999.9999999999998863 ) ;
#1497=AXIS2_PLACEMENT_3D ( 'NONE', #89913, #79094, #11614 ) ;
#1499=ORIENTED_EDGE ( 'NONE', *, *, #12379, .F. ) ;
#1501=DIRECTION ( 'NONE',  ( -0.7071067811865486830, -0.7071067811865464625, 0.000000000000000000 ) ) ;
#1502=EDGE_LOOP ( 'NONE', ( #118836, #140359, #24138, #67306, #53247, #41866 ) ) ;
#1503=CARTESIAN_POINT ( 'NONE',  ( 0.7933393645784738712, 21.75929247661549937, 4.998822639870705409 ) ) ;
#1504=DIRECTION ( 'NONE',  ( -0.7071067811865486830, -0.7071067811865464625, 0.000000000000000000 ) ) ;
#1505=VECTOR ( 'NONE', #40511, 1000.000000000000227 ) ;
#1506=CARTESIAN_POINT ( 'NONE',  ( 34.17183060077623225, 6.759292476615649470, 4.000000000000000000 ) ) ;
#1507=DIRECTION ( 'NONE',  ( -0.7071067811865487940, 0.7071067811865463515, -0.000000000000000000 ) ) ;
#1509=CARTESIAN_POINT ( 'NONE',  ( -8.206660635421469507, 21.75929247661548516, 4.998822639870715179 ) ) ;
#1510=ORIENTED_EDGE ( 'NONE', *, *, #84750, .T. ) ;
#1511=VERTEX_POINT ( 'NONE', #60945 ) ;
#1512=ORIENTED_EDGE ( 'NONE', *, *, #137577, .F. ) ;
#1513=ORIENTED_EDGE ( 'NONE', *, *, #78402, .F. ) ;
#1514=DIRECTION ( 'NONE',  ( 0.7071067811865487940, 0.7071067811865463515, 0.000000000000000000 ) ) ;
#1515=DIRECTION ( 'NONE',  ( -0.7071067811865487940, 0.7071067811865463515, -0.000000000000000000 ) ) ;
#1516=EDGE_LOOP ( 'NONE', ( #43037, #113889, #1371, #10256 ) ) ;
#1517=ORIENTED_EDGE ( 'NONE', *, *, #98319, .F. ) ;
#1518=CARTESIAN_POINT ( 'NONE',  ( 34.49999999999976552, -20.56887692260760758, 4.000000000000000000 ) ) ;
#1519=EDGE_CURVE ( 'NONE', #132460, #13150, #118831, .T. ) ;
#1520=EDGE_CURVE ( 'NONE', #95429, #71113, #90370, .T. ) ;
#1522=ORIENTED_EDGE ( 'NONE', *, *, #12001, .F. ) ;
#1523=DIRECTION ( 'NONE',  ( -0.7071067811865486830, -0.7071067811865464625, 0.000000000000000000 ) ) ;
#1526=AXIS2_PLACEMENT_3D ( 'NONE', #100709, #35484, #34032 ) ;
#1527=CARTESIAN_POINT ( 'NONE',  ( 18.29974487139159223, -27.71228299555219010, 4.000000000000000000 ) ) ;
#1528=ORIENTED_EDGE ( 'NONE', *, *, #23028, .T. ) ;
#1530=ADVANCED_FACE ( 'NONE', ( #39883 ), #5765, .F. ) ;
#1531=CARTESIAN_POINT ( 'NONE',  ( -19.82816939922339117, -20.24070752338407075, 4.000000000000000000 ) ) ;
#1532=CARTESIAN_POINT ( 'NONE',  ( -22.49999999999984368, -17.56887692260762535, 4.000000000000000000 ) ) ;
#1533=CARTESIAN_POINT ( 'NONE',  ( -20.29289321881331887, 20.25929247661551713, 5.000000000000000000 ) ) ;
#1535=VERTEX_POINT ( 'NONE', #126840 ) ;
#1536=VECTOR ( 'NONE', #139144, 1000.000000000000000 ) ;
#1538=ORIENTED_EDGE ( 'NONE', *, *, #91976, .F. ) ;
#1539=CARTESIAN_POINT ( 'NONE',  ( 0.000000000000000000, 0.000000000000000000, 5.000000000000000000 ) ) ;
#1541=EDGE_CURVE ( 'NONE', #41257, #28318, #118084, .T. ) ;
#1543=CARTESIAN_POINT ( 'NONE',  ( 54.29974487139159578, -27.71228299555243879, 4.000000000000000000 ) ) ;
#1544=FACE_OUTER_BOUND ( 'NONE', #84083, .T. ) ;
#1545=VECTOR ( 'NONE', #129995, 999.9999999999998863 ) ;
#1546=ORIENTED_EDGE ( 'NONE', *, *, #130615, .T. ) ;
#1547=CARTESIAN_POINT ( 'NONE',  ( 75.29974487139158157, -27.71228299555258445, 4.000000000000000000 ) ) ;
#1548=ORIENTED_EDGE ( 'NONE', *, *, #13366, .F. ) ;
#1549=LINE ( 'NONE', #133543, #97033 ) ;
#1550=LINE ( 'NONE', #67599, #127337 ) ;
#1551=ORIENTED_EDGE ( 'NONE', *, *, #11047, .F. ) ;
#1552=ORIENTED_EDGE ( 'NONE', *, *, #115524, .T. ) ;
#1554=LINE ( 'NONE', #134264, #113081 ) ;
#1555=ORIENTED_EDGE ( 'NONE', *, *, #87944, .T. ) ;
#1557=CARTESIAN_POINT ( 'NONE',  ( -15.48921356237309510, -27.52281430457066236, 5.000000000000000000 ) ) ;
#1558=EDGE_CURVE ( 'NONE', #44425, #11674, #7911, .T. ) ;
#1559=EDGE_CURVE ( 'NONE', #80500, #142230, #138460, .T. ) ;
#1561=PLANE ( 'NONE',  #90822 ) ;
#1563=ORIENTED_EDGE ( 'NONE', *, *, #9139, .F. ) ;
#1564=EDGE_CURVE ( 'NONE', #110396, #16938, #6452, .T. ) ;
#1565=CARTESIAN_POINT ( 'NONE',  ( 47.99451991528749062, 28.92564299267971251, 4.000000000000000000 ) ) ;
#1566=DIRECTION ( 'NONE',  ( -1.000000000000000000, 0.000000000000000000, 0.000000000000000000 ) ) ;
#1567=FACE_OUTER_BOUND ( 'NONE', #2043, .T. ) ;
#1569=CARTESIAN_POINT ( 'NONE',  ( 0.000000000000000000, 0.000000000000000000, 5.000000000000000000 ) ) ;
#1570=DIRECTION ( 'NONE',  ( -0.7071067811865486830, -0.7071067811865464625, -0.000000000000000000 ) ) ;
#1571=EDGE_CURVE ( 'NONE', #118176, #99074, #74643, .T. ) ;
#1572=ORIENTED_EDGE ( 'NONE', *, *, #136943, .T. ) ;
#1573=EDGE_CURVE ( 'NONE', #20152, #38617, #18052, .T. ) ;
#1574=ORIENTED_EDGE ( 'NONE', *, *, #63399, .T. ) ;
#1575=ORIENTED_EDGE ( 'NONE', *, *, #68045, .F. ) ;
#1576=CARTESIAN_POINT ( 'NONE',  ( -23.29289321881329400, -15.74070752338412049, 5.000000000000000000 ) ) ;
#1577=ORIENTED_EDGE ( 'NONE', *, *, #16284, .T. ) ;
#1578=ORIENTED_EDGE ( 'NONE', *, *, #55938, .F. ) ;
#1579=ORIENTED_EDGE ( 'NONE', *, *, #33468, .F. ) ;
#1580=DIRECTION ( 'NONE',  ( 0.3543493200069163240, 0.000000000000000000, -0.9351131265310288487 ) ) ;
#1581=LINE ( 'NONE', #45167, #37017 ) ;
#1582=ORIENTED_EDGE ( 'NONE', *, *, #59458, .T. ) ;
#1585=CARTESIAN_POINT ( 'NONE',  ( -9.489213562373095101, -27.52281430457062328, 5.000000000000000000 ) ) ;
#1586=VECTOR ( 'NONE', #105774, 999.9999999999998863 ) ;
#1587=ADVANCED_FACE ( 'NONE', ( #120969 ), #132611, .F. ) ;
#1588=CARTESIAN_POINT ( 'NONE',  ( 34.49999999999976552, 7.087461875839180081, 4.000000000000000000 ) ) ;
#1590=ORIENTED_EDGE ( 'NONE', *, *, #135957, .F. ) ;
#1591=ADVANCED_FACE ( 'NONE', ( #44148 ), #120223, .F. ) ;
#1592=PLANE ( 'NONE',  #46502 ) ;
#1593=CARTESIAN_POINT ( 'NONE',  ( 48.29974487139158867, -27.71228299555239971, 4.000000000000000000 ) ) ;
#1594=CARTESIAN_POINT ( 'NONE',  ( -27.65671000166196336, 3.759292476615681888, 13.27625715073259194 ) ) ;
#1595=DIRECTION ( 'NONE',  ( -0.7071067811865486830, 0.7071067811865464625, 0.000000000000000000 ) ) ;
#1596=DIRECTION ( 'NONE',  ( -0.6830127018922180770, -0.6830127018922204085, -0.2588190451025213501 ) ) ;
#1598=AXIS2_PLACEMENT_3D ( 'NONE', #139895, #16649, #118072 ) ;
#1600=CARTESIAN_POINT ( 'NONE',  ( 5.994519915287488843, 28.92564299267942118, 4.000000000000000000 ) ) ;
#1601=AXIS2_PLACEMENT_3D ( 'NONE', #26769, #94857, #16595 ) ;
#1603=ORIENTED_EDGE ( 'NONE', *, *, #31102, .T. ) ;
#1604=ORIENTED_EDGE ( 'NONE', *, *, #23536, .T. ) ;
#1606=EDGE_CURVE ( 'NONE', #101542, #107149, #122389, .T. ) ;
#1607=PLANE ( 'NONE',  #55491 ) ;
#1609=VERTEX_POINT ( 'NONE', #53599 ) ;
#1610=EDGE_CURVE ( 'NONE', #23253, #53228, #142047, .T. ) ;
#1611=DIRECTION ( 'NONE',  ( -0.000000000000000000, 0.3543493200069153248, 0.9351131265310292928 ) ) ;
#1612=DIRECTION ( 'NONE',  ( 0.6830127018922181881, 0.6830127018922202975, -0.2588190451025214056 ) ) ;
#1614=EDGE_LOOP ( 'NONE', ( #29287, #108877, #10108, #69457 ) ) ;
#1615=ORIENTED_EDGE ( 'NONE', *, *, #82787, .F. ) ;
#1616=EDGE_CURVE ( 'NONE', #82699, #69434, #59662, .T. ) ;
#1617=DIRECTION ( 'NONE',  ( -0.000000000000000000, 0.3543493200069153248, 0.9351131265310291818 ) ) ;
#1620=CARTESIAN_POINT ( 'NONE',  ( 8.510786437626906675, -27.52281430457049183, 5.000000000000000000 ) ) ;
#1621=ORIENTED_EDGE ( 'NONE', *, *, #24503, .F. ) ;
#1622=CARTESIAN_POINT ( 'NONE',  ( 0.000000000000000000, 0.000000000000000000, 5.000000000000000000 ) ) ;
#1623=EDGE_LOOP ( 'NONE', ( #19991, #131981, #32246, #39871 ) ) ;
#1624=CARTESIAN_POINT ( 'NONE',  ( -21.70679250724060694, 20.25929247661551358, 20.83292124670819945 ) ) ;
#1625=CARTESIAN_POINT ( 'NONE',  ( -17.99451991528748351, 28.92564299267950645, 4.000000000000000000 ) ) ;
#1626=CARTESIAN_POINT ( 'NONE',  ( 14.99999999999989875, 12.83542986846998524, -1.025386466790403794 ) ) ;
#1628=VECTOR ( 'NONE', #36666, 1000.000000000000000 ) ;
#1629=ADVANCED_FACE ( 'NONE', ( #78207 ), #99948, .F. ) ;
#1630=DIRECTION ( 'NONE',  ( -0.000000000000000000, 0.3543493200069153248, 0.9351131265310292928 ) ) ;
#1631=CARTESIAN_POINT ( 'NONE',  ( -14.27718569542929572, -21.72500000000000142, 5.000000000000000000 ) ) ;
#1632=EDGE_CURVE ( 'NONE', #89964, #137620, #86935, .T. ) ;
#1633=ORIENTED_EDGE ( 'NONE', *, *, #32152, .F. ) ;
#1634=AXIS2_PLACEMENT_3D ( 'NONE', #4478, #124902, #27010 ) ;
#1635=DIRECTION ( 'NONE',  ( 1.000000000000000000, 0.000000000000000000, 0.000000000000000000 ) ) ;
#1637=FACE_OUTER_BOUND ( 'NONE', #32238, .T. ) ;
#1638=LINE ( 'NONE', #33623, #110266 ) ;
#1640=ORIENTED_EDGE ( 'NONE', *, *, #64059, .T. ) ;
#1642=FACE_OUTER_BOUND ( 'NONE', #17218, .T. ) ;
#1643=EDGE_CURVE ( 'NONE', #48159, #126178, #54335, .T. ) ;
#1646=VERTEX_POINT ( 'NONE', #108636 ) ;
#1647=CARTESIAN_POINT ( 'NONE',  ( -10.49999999999993250, 9.431123077392092213, 4.000000000000000000 ) ) ;
#1648=CARTESIAN_POINT ( 'NONE',  ( -22.17183060077631396, -20.24070752338407786, 4.000000000000000000 ) ) ;
#1650=DIRECTION ( 'NONE',  ( -0.000000000000000000, 0.3543493200069153248, 0.9351131265310292928 ) ) ;
#1651=DIRECTION ( 'NONE',  ( 0.3543493200069162685, -0.000000000000000000, -0.9351131265310288487 ) ) ;
#1652=FACE_BOUND ( 'NONE', #21354, .T. ) ;
#1653=CARTESIAN_POINT ( 'NONE',  ( 34.92499999999998295, 3.006123077391939624, 4.000000000000000000 ) ) ;
#1654=CARTESIAN_POINT ( 'NONE',  ( 17.99999999999987566, -11.35517001088070366, -1.126524801160067479 ) ) ;
#1655=CARTESIAN_POINT ( 'NONE',  ( -0.7071067811865415775, 14.25929247661557397, 5.000000000000000000 ) ) ;
#1656=LINE ( 'NONE', #111143, #4130 ) ;
#1658=DIRECTION ( 'NONE',  ( 0.6830127018922181881, 0.6830127018922202975, -0.2588190451025214056 ) ) ;
#1659=VERTEX_POINT ( 'NONE', #97039 ) ;
#1662=ORIENTED_EDGE ( 'NONE', *, *, #90642, .F. ) ;
#1663=DIRECTION ( 'NONE',  ( 0.7071067811865487940, 0.7071067811865463515, 0.000000000000000000 ) ) ;
#1665=ORIENTED_EDGE ( 'NONE', *, *, #13788, .F. ) ;
#1666=DIRECTION ( 'NONE',  ( 0.7071067811865487940, 0.7071067811865463515, 0.000000000000000000 ) ) ;
#1667=DIRECTION ( 'NONE',  ( 0.7071067811865487940, -0.7071067811865463515, 0.000000000000000000 ) ) ;
#1669=LINE ( 'NONE', #80037, #29651 ) ;
#1670=CARTESIAN_POINT ( 'NONE',  ( 57.18398860626899705, 28.73617430169827358, 5.000000000000000000 ) ) ;
#1674=VERTEX_POINT ( 'NONE', #20936 ) ;
#1675=CARTESIAN_POINT ( 'NONE',  ( -6.183988606268994381, 28.73617430169791476, 5.000000000000000000 ) ) ;
#1676=CARTESIAN_POINT ( 'NONE',  ( 16.49999999999988276, -19.53360074219753884, 5.000000000000000000 ) ) ;
#1677=ORIENTED_EDGE ( 'NONE', *, *, #96020, .T. ) ;
#1678=ORIENTED_EDGE ( 'NONE', *, *, #119738, .T. ) ;
#1679=VECTOR ( 'NONE', #128806, 999.9999999999998863 ) ;
#1681=ADVANCED_FACE ( 'NONE', ( #99196 ), #119515, .F. ) ;
#1682=EDGE_CURVE ( 'NONE', #98221, #131683, #65923, .T. ) ;
#1683=LINE ( 'NONE', #88030, #104022 ) ;
#1685=DIRECTION ( 'NONE',  ( -0.3543493200069162685, -0.000000000000000000, -0.9351131265310288487 ) ) ;
#1686=VECTOR ( 'NONE', #62693, 1000.000000000000000 ) ;
#1691=CARTESIAN_POINT ( 'NONE',  ( 18.18398860626898994, 28.73617430169800002, 5.000000000000000000 ) ) ;
#1693=EDGE_CURVE ( 'NONE', #52394, #129216, #31831, .T. ) ;
#1694=DIRECTION ( 'NONE',  ( -1.000000000000000000, 0.000000000000000000, 0.000000000000000000 ) ) ;
#1695=VECTOR ( 'NONE', #83896, 1000.000000000000000 ) ;
#1696=CYLINDRICAL_SURFACE ( 'NONE', #100786, 0.5000000000000004441 ) ;
#1697=CARTESIAN_POINT ( 'NONE',  ( -34.92500000000001137, 22.22500000000000142, 4.000000000000000000 ) ) ;
#1698=ORIENTED_EDGE ( 'NONE', *, *, #97815, .F. ) ;
#1699=ORIENTED_EDGE ( 'NONE', *, *, #53805, .T. ) ;
#1700=CARTESIAN_POINT ( 'NONE',  ( 26.99999999999981526, -4.068876922607768343, 4.000000000000000000 ) ) ;
#1702=EDGE_CURVE ( 'NONE', #79902, #3869, #143436, .T. ) ;
#1704=CARTESIAN_POINT ( 'NONE',  ( 0.000000000000000000, 0.000000000000000000, 5.000000000000000000 ) ) ;
#1705=CARTESIAN_POINT ( 'NONE',  ( 33.18398860626899705, 28.73617430169810305, 5.000000000000000000 ) ) ;
#1706=CARTESIAN_POINT ( 'NONE',  ( -32.99999999999977263, 16.55218569542899587, 5.000000000000000000 ) ) ;
#1707=CARTESIAN_POINT ( 'NONE',  ( 30.29974487139158867, -27.71228299555227537, 4.000000000000000000 ) ) ;
#1708=DIRECTION ( 'NONE',  ( -0.7071067811865486830, -0.7071067811865464625, 0.000000000000000000 ) ) ;
#1709=EDGE_CURVE ( 'NONE', #103522, #39262, #65203, .T. ) ;
#1710=DIRECTION ( 'NONE',  ( -0.000000000000000000, -0.3543493200069152693, 0.9351131265310292928 ) ) ;
#1711=LINE ( 'NONE', #46005, #139612 ) ;
#1712=( BOUNDED_CURVE ( )  B_SPLINE_CURVE ( 3, ( #120647, #21366, #129390, #65627 ),
 .UNSPECIFIED., .F., .T. ) 
 B_SPLINE_CURVE_WITH_KNOTS ( ( 4, 4 ),
 ( 5.106027341939290309, 6.645403452391245303 ),
 .UNSPECIFIED. ) 
 CURVE ( )  GEOMETRIC_REPRESENTATION_ITEM ( )  RATIONAL_B_SPLINE_CURVE ( ( 1.000000000000000000, 0.8120851936182301722, 0.8120851936182301722, 1.000000000000000000 ) ) 
 REPRESENTATION_ITEM ( '' )  );
#1713=CARTESIAN_POINT ( 'NONE',  ( -29.99451991528749417, 28.92564299267958816, 4.000000000000000000 ) ) ;
#1714=LINE ( 'NONE', #24927, #21617 ) ;
#1715=LINE ( 'NONE', #124964, #73800 ) ;
#1716=ORIENTED_EDGE ( 'NONE', *, *, #58492, .T. ) ;
#1717=ORIENTED_EDGE ( 'NONE', *, *, #28800, .T. ) ;
#1718=VECTOR ( 'NONE', #35110, 1000.000000000000000 ) ;
#1719=ADVANCED_FACE ( 'NONE', ( #55742 ), #133309, .F. ) ;
#1720=PLANE ( 'NONE',  #131344 ) ;
#1723=VECTOR ( 'NONE', #137650, 1000.000000000000000 ) ;
#1725=DIRECTION ( 'NONE',  ( -0.7071067811865486830, -0.7071067811865464625, 0.000000000000000000 ) ) ;
#1726=CARTESIAN_POINT ( 'NONE',  ( -3.489213562373097322, -27.52281430457057709, 5.000000000000000000 ) ) ;
#1727=CARTESIAN_POINT ( 'NONE',  ( 13.11547925347946908, 3.815643823912585386, 4.000000000000000000 ) ) ;
#1728=ORIENTED_EDGE ( 'NONE', *, *, #127304, .F. ) ;
#1729=EDGE_CURVE ( 'NONE', #126528, #115378, #92612, .T. ) ;
#1730=CARTESIAN_POINT ( 'NONE',  ( 25.49999999999982236, 11.52377502935405040, -1.522421517564144677 ) ) ;
#1731=CARTESIAN_POINT ( 'NONE',  ( -17.99999999999986855, -12.03360074219761700, 5.000000000000000000 ) ) ;
#1735=FACE_OUTER_BOUND ( 'NONE', #37412, .T. ) ;
#1736=EDGE_CURVE ( 'NONE', #13171, #91632, #91912, .T. ) ;
#1737=EDGE_CURVE ( 'NONE', #29835, #121898, #14362, .T. ) ;
#1739=ORIENTED_EDGE ( 'NONE', *, *, #63831, .T. ) ;
#1740=LINE ( 'NONE', #88821, #118233 ) ;
#1741=ORIENTED_EDGE ( 'NONE', *, *, #83327, .T. ) ;
#1742=CARTESIAN_POINT ( 'NONE',  ( 9.773048296453090700, -22.22500000000000142, -11.93776140031427602 ) ) ;
#1743=ADVANCED_FACE ( 'NONE', ( #47745 ), #12913, .T. ) ;
#1745=DIRECTION ( 'NONE',  ( -0.7071067811865486830, -0.7071067811865464625, 0.000000000000000000 ) ) ;
#1746=DIRECTION ( 'NONE',  ( 0.7071067811865487940, -0.7071067811865463515, 0.000000000000000000 ) ) ;
#1747=EDGE_CURVE ( 'NONE', #65901, #96557, #134750, .T. ) ;
#1748=CARTESIAN_POINT ( 'NONE',  ( 17.20666063542140733, 21.75929247661550292, 4.998822639870701856 ) ) ;
#1749=CARTESIAN_POINT ( 'NONE',  ( -34.92500000000001137, 16.70193056682083821, 4.500000000000000888 ) ) ;
#1750=EDGE_LOOP ( 'NONE', ( #22599, #112914, #20807, #113972 ) ) ;
#1752=LINE ( 'NONE', #24960, #2657 ) ;
#1753=CARTESIAN_POINT ( 'NONE',  ( -30.70710678118632231, 2.259292476615694323, 5.000000000000000000 ) ) ;
#1754=CARTESIAN_POINT ( 'NONE',  ( -21.32816939922336985, -6.740707523384218192, 4.000000000000000000 ) ) ;
#1755=LINE ( 'NONE', #143198, #115332 ) ;
#1757=CARTESIAN_POINT ( 'NONE',  ( -1.499999999999977129, 4.087461875839200509, 4.000000000000000000 ) ) ;
#1759=ORIENTED_EDGE ( 'NONE', *, *, #15923, .F. ) ;
#1760=VECTOR ( 'NONE', #139576, 1000.000000000000000 ) ;
#1762=EDGE_CURVE ( 'NONE', #28277, #97071, #2761, .T. ) ;
#1764=CARTESIAN_POINT ( 'NONE',  ( -48.48921356237309510, -27.52281430457089328, 5.000000000000000000 ) ) ;
#1765=LINE ( 'NONE', #89536, #119185 ) ;
#1766=EDGE_LOOP ( 'NONE', ( #106955, #105624, #92568, #12610 ) ) ;
#1767=EDGE_CURVE ( 'NONE', #9326, #100143, #125539, .T. ) ;
#1768=CARTESIAN_POINT ( 'NONE',  ( -30.70710678118633652, -6.740707523384211086, 5.000000000000000000 ) ) ;
#1770=CARTESIAN_POINT ( 'NONE',  ( -19.05000000000000071, 3.174999999999997158, 4.000000000000000000 ) ) ;
#1772=ORIENTED_EDGE ( 'NONE', *, *, #17406, .T. ) ;
#1773=ORIENTED_EDGE ( 'NONE', *, *, #82459, .T. ) ;
#1774=VECTOR ( 'NONE', #115632, 1000.000000000000000 ) ;
#1776=CARTESIAN_POINT ( 'NONE',  ( 6.156123077392376963, -22.22500000000000142, 4.000000000000000000 ) ) ;
#1777=VECTOR ( 'NONE', #117043, 999.9999999999998863 ) ;
#1778=CARTESIAN_POINT ( 'NONE',  ( 8.683420388672054457, -6.740707523384212863, 11.88629033278122371 ) ) ;
#1779=DIRECTION ( 'NONE',  ( 0.6830127018922180770, -0.6830127018922204085, -0.2588190451025213501 ) ) ;
#1780=CARTESIAN_POINT ( 'NONE',  ( 3.299744871391591339, -27.71228299555208352, 4.000000000000000000 ) ) ;
#1783=CARTESIAN_POINT ( 'NONE',  ( -21.48921356237309155, -27.52281430457070499, 5.000000000000000000 ) ) ;
#1784=LINE ( 'NONE', #385, #98027 ) ;
#1785=AXIS2_PLACEMENT_3D ( 'NONE', #35089, #112621, #3130 ) ;
#1786=PLANE ( 'NONE',  #115501 ) ;
#1787=VECTOR ( 'NONE', #44345, 1000.000000000000000 ) ;
#1788=VERTEX_POINT ( 'NONE', #47059 ) ;
#1790=EDGE_LOOP ( 'NONE', ( #29145, #85466, #31293, #139892 ) ) ;
#1793=FACE_OUTER_BOUND ( 'NONE', #42063, .T. ) ;
#1794=ADVANCED_FACE ( 'NONE', ( #106327 ), #93350, .F. ) ;
#1795=CARTESIAN_POINT ( 'NONE',  ( 33.18398860626899705, 28.73617430169810305, 5.000000000000000000 ) ) ;
#1797=DIRECTION ( 'NONE',  ( -0.7071067811865486830, -0.7071067811865464625, -0.000000000000000000 ) ) ;
#1798=CARTESIAN_POINT ( 'NONE',  ( 32.29289321881323360, 14.25929247661557397, 5.000000000000000000 ) ) ;
#1801=CARTESIAN_POINT ( 'NONE',  ( -9.183988606268997046, 28.73617430169793607, 5.000000000000000000 ) ) ;
#1803=VERTEX_POINT ( 'NONE', #51995 ) ;
#1804=CARTESIAN_POINT ( 'NONE',  ( -35.99451991528749772, 28.92564299267963079, 4.000000000000000000 ) ) ;
#1806=PLANE ( 'NONE',  #118803 ) ;
#1807=EDGE_LOOP ( 'NONE', ( #12046, #120511, #128816, #44564 ) ) ;
#1808=FACE_BOUND ( 'NONE', #103518, .T. ) ;
#1809=CARTESIAN_POINT ( 'NONE',  ( 23.67183060077630685, -18.74070752338408852, 4.000000000000000000 ) ) ;
#1810=CARTESIAN_POINT ( 'NONE',  ( 0.000000000000000000, 21.72500000000000142, 4.500000000000000888 ) ) ;
#1811=LINE ( 'NONE', #78723, #89881 ) ;
#1812=VECTOR ( 'NONE', #141508, 1000.000000000000000 ) ;
#1813=DIRECTION ( 'NONE',  ( -0.000000000000000000, 0.000000000000000000, 1.000000000000000000 ) ) ;
#1814=DIRECTION ( 'NONE',  ( -0.7071067811865486830, -0.7071067811865464625, 0.000000000000000000 ) ) ;
#1817=ORIENTED_EDGE ( 'NONE', *, *, #37742, .T. ) ;
#1820=ORIENTED_EDGE ( 'NONE', *, *, #126955, .F. ) ;
#1821=DIRECTION ( 'NONE',  ( -0.6830127018922180770, -0.6830127018922204085, -0.2588190451025213501 ) ) ;
#1822=ORIENTED_EDGE ( 'NONE', *, *, #97515, .F. ) ;
#1823=DIRECTION ( 'NONE',  ( -1.000000000000000000, 0.000000000000000000, 0.000000000000000000 ) ) ;
#1825=AXIS2_PLACEMENT_3D ( 'NONE', #125722, #80092, #24940 ) ;
#1826=CARTESIAN_POINT ( 'NONE',  ( -5.149948714589728915, -8.240707523384200428, 17.25253755692238045 ) ) ;
#1827=ORIENTED_EDGE ( 'NONE', *, *, #5420, .T. ) ;
#1829=LINE ( 'NONE', #33134, #132951 ) ;
#1830=CARTESIAN_POINT ( 'NONE',  ( -24.48921356237309510, -27.52281430457072631, 5.000000000000000000 ) ) ;
#1832=CARTESIAN_POINT ( 'NONE',  ( 27.18398860626900060, 28.73617430169806042, 5.000000000000000000 ) ) ;
#1833=CARTESIAN_POINT ( 'NONE',  ( -9.183988606268997046, 28.73617430169793607, 5.000000000000000000 ) ) ;
#1834=LINE ( 'NONE', #2580, #127794 ) ;
#1835=ORIENTED_EDGE ( 'NONE', *, *, #137418, .F. ) ;
#1836=CARTESIAN_POINT ( 'NONE',  ( -6.328169399223481761, -21.74070752338406365, 4.000000000000000000 ) ) ;
#1837=LINE ( 'NONE', #33829, #212 ) ;
#1838=EDGE_CURVE ( 'NONE', #135322, #113494, #38966, .T. ) ;
#1839=VERTEX_POINT ( 'NONE', #82484 ) ;
#1840=EDGE_LOOP ( 'NONE', ( #96030, #136405, #78599, #23348 ) ) ;
#1841=EDGE_CURVE ( 'NONE', #106517, #37184, #29500, .T. ) ;
#1842=ADVANCED_FACE ( 'NONE', ( #41108 ), #139007, .F. ) ;
#1843=ORIENTED_EDGE ( 'NONE', *, *, #82528, .F. ) ;
#1845=ORIENTED_EDGE ( 'NONE', *, *, #72695, .F. ) ;
#1846=EDGE_CURVE ( 'NONE', #16129, #113816, #38263, .T. ) ;
#1847=EDGE_CURVE ( 'NONE', #93168, #108750, #28817, .T. ) ;
#1848=DIRECTION ( 'NONE',  ( -0.7071067811865486830, 0.7071067811865464625, 0.000000000000000000 ) ) ;
#1850=AXIS2_PLACEMENT_3D ( 'NONE', #129361, #43799, #119892 ) ;
#1852=CARTESIAN_POINT ( 'NONE',  ( -78.48921356237309510, -27.52281430457109934, 5.000000000000000000 ) ) ;
#1853=EDGE_LOOP ( 'NONE', ( #108366, #141116, #110679, #48056 ) ) ;
#1854=EDGE_CURVE ( 'NONE', #75714, #41182, #129526, .T. ) ;
#1855=CARTESIAN_POINT ( 'NONE',  ( -32.20710678118631876, 0.7592924766157104211, 5.000000000000000000 ) ) ;
#1856=ORIENTED_EDGE ( 'NONE', *, *, #134942, .T. ) ;
#1858=CARTESIAN_POINT ( 'NONE',  ( 51.48921356237309510, -27.52281430457091460, 5.000000000000000000 ) ) ;
#1860=PLANE ( 'NONE',  #34474 ) ;
#1861=DIRECTION ( 'NONE',  ( 1.000000000000000000, 0.000000000000000000, 0.000000000000000000 ) ) ;
#1862=EDGE_CURVE ( 'NONE', #55140, #78905, #60023, .T. ) ;
#1863=ORIENTED_EDGE ( 'NONE', *, *, #76673, .F. ) ;
#1864=DIRECTION ( 'NONE',  ( -0.7071067811865487940, 0.7071067811865463515, -0.000000000000000000 ) ) ;
#1865=ORIENTED_EDGE ( 'NONE', *, *, #43373, .F. ) ;
#1867=ORIENTED_EDGE ( 'NONE', *, *, #125021, .T. ) ;
#1868=EDGE_CURVE ( 'NONE', #22900, #79079, #30247, .T. ) ;
#1869=VECTOR ( 'NONE', #52045, 1000.000000000000000 ) ;
#1870=VECTOR ( 'NONE', #61137, 1000.000000000000000 ) ;
#1871=DIRECTION ( 'NONE',  ( 0.7071067811865487940, 0.7071067811865463515, 0.000000000000000000 ) ) ;
#1872=LINE ( 'NONE', #124421, #106488 ) ;
#1873=DIRECTION ( 'NONE',  ( 0.6830127018922180770, -0.6830127018922204085, -0.2588190451025213501 ) ) ;
#1874=ORIENTED_EDGE ( 'NONE', *, *, #45875, .T. ) ;
#1875=EDGE_CURVE ( 'NONE', #30242, #132436, #7743, .T. ) ;
#1876=EDGE_CURVE ( 'NONE', #109399, #16896, #4856, .T. ) ;
#1877=AXIS2_PLACEMENT_3D ( 'NONE', #42932, #55954, #120423 ) ;
#1878=AXIS2_PLACEMENT_3D ( 'NONE', #106341, #115778, #17899 ) ;
#1879=DIRECTION ( 'NONE',  ( -0.000000000000000000, 0.000000000000000000, 1.000000000000000000 ) ) ;
#1880=( BOUNDED_CURVE ( )  B_SPLINE_CURVE ( 3, ( #114115, #125727, #59759, #80096 ),
 .UNSPECIFIED., .F., .T. ) 
 B_SPLINE_CURVE_WITH_KNOTS ( ( 4, 4 ),
 ( 2.779374508378134045, 4.199602562396838934 ),
 .UNSPECIFIED. ) 
 CURVE ( )  GEOMETRIC_REPRESENTATION_ITEM ( )  RATIONAL_B_SPLINE_CURVE ( ( 1.000000000000000000, 0.8388583629366626049, 0.8388583629366626049, 1.000000000000000000 ) ) 
 REPRESENTATION_ITEM ( '' )  );
#1882=CARTESIAN_POINT ( 'NONE',  ( 14.99999999999989342, -13.97847968911258931, -0.1324546996126444443 ) ) ;
#1883=DIRECTION ( 'NONE',  ( 0.3543493200069162685, -0.000000000000000000, -0.9351131265310288487 ) ) ;
#1886=VERTEX_POINT ( 'NONE', #83192 ) ;
#1887=EDGE_CURVE ( 'NONE', #57582, #134641, #71607, .T. ) ;
#1890=CARTESIAN_POINT ( 'NONE',  ( 0.000000000000000000, 0.000000000000000000, 0.000000000000000000 ) ) ;
#1892=FACE_OUTER_BOUND ( 'NONE', #24783, .T. ) ;
#1894=CARTESIAN_POINT ( 'NONE',  ( 0.000000000000000000, 0.000000000000000000, 5.000000000000000000 ) ) ;
#1895=ADVANCED_FACE ( 'NONE', ( #16470 ), #60770, .F. ) ;
#1896=VECTOR ( 'NONE', #89011, 1000.000000000000000 ) ;
#1897=CARTESIAN_POINT ( 'NONE',  ( 9.005480084712511157, 28.92564299267931816, 4.000000000000000000 ) ) ;
#1900=CARTESIAN_POINT ( 'NONE',  ( -24.48921356237309510, -27.52281430457072631, 5.000000000000000000 ) ) ;
#1901=ADVANCED_FACE ( 'NONE', ( #28093 ), #72360, .F. ) ;
#1902=LINE ( 'NONE', #504, #115948 ) ;
#1903=ORIENTED_EDGE ( 'NONE', *, *, #103057, .F. ) ;
#1904=VECTOR ( 'NONE', #36226, 1000.000000000000227 ) ;
#1906=ORIENTED_EDGE ( 'NONE', *, *, #19958, .T. ) ;
#1908=EDGE_CURVE ( 'NONE', #51825, #93361, #134880, .T. ) ;
#1910=CARTESIAN_POINT ( 'NONE',  ( 8.510786437626906675, -27.52281430457049183, 5.000000000000000000 ) ) ;
#1911=DIRECTION ( 'NONE',  ( 0.7071067811865486830, -0.7071067811865464625, -0.000000000000000000 ) ) ;
#1912=EDGE_LOOP ( 'NONE', ( #110003, #108495, #107348, #26014 ) ) ;
#1914=CARTESIAN_POINT ( 'NONE',  ( 7.499999999999951150, -6.839392718269120763, -8.480912228396103814 ) ) ;
#1915=ORIENTED_EDGE ( 'NONE', *, *, #99339, .T. ) ;
#1916=LINE ( 'NONE', #34603, #4461 ) ;
#1918=CARTESIAN_POINT ( 'NONE',  ( -3.489213562373097322, -27.52281430457057709, 5.000000000000000000 ) ) ;
#1919=ORIENTED_EDGE ( 'NONE', *, *, #78418, .T. ) ;
#1924=CARTESIAN_POINT ( 'NONE',  ( 19.49999999999986144, 9.127013188829479873, 4.802533355213541633 ) ) ;
#1925=ORIENTED_EDGE ( 'NONE', *, *, #126778, .F. ) ;
#1926=EDGE_CURVE ( 'NONE', #16100, #41563, #54172, .T. ) ;
#1927=DIRECTION ( 'NONE',  ( -0.7071067811865486830, -0.7071067811865464625, 0.000000000000000000 ) ) ;
#1928=CARTESIAN_POINT ( 'NONE',  ( -19.21498419724177609, -3.740707523384238176, 15.76143240460119443 ) ) ;
#1929=CARTESIAN_POINT ( 'NONE',  ( -2.510786437626908008, -27.52281430457053446, 5.000000000000000000 ) ) ;
#1932=VECTOR ( 'NONE', #59352, 1000.000000000000000 ) ;
#1933=DIRECTION ( 'NONE',  ( -0.7071067811865486830, -0.7071067811865464625, 0.000000000000000000 ) ) ;
#1934=CARTESIAN_POINT ( 'NONE',  ( -29.27718569542920335, -21.72500000000000142, 5.000000000000000000 ) ) ;
#1935=ORIENTED_EDGE ( 'NONE', *, *, #50749, .T. ) ;
#1936=VECTOR ( 'NONE', #30691, 1000.000000000000000 ) ;
#1937=PLANE ( 'NONE',  #136965 ) ;
#1940=DIRECTION ( 'NONE',  ( 0.7071067811865487940, -0.7071067811865463515, 0.000000000000000000 ) ) ;
#1942=DIRECTION ( 'NONE',  ( -0.6830127018922180770, -0.6830127018922204085, -0.2588190451025213501 ) ) ;
#1944=ORIENTED_EDGE ( 'NONE', *, *, #142379, .T. ) ;
#1945=FACE_OUTER_BOUND ( 'NONE', #78347, .T. ) ;
#1946=CARTESIAN_POINT ( 'NONE',  ( -19.49999999999985789, -13.91253812416061386, 4.000000000000000000 ) ) ;
#1947=DIRECTION ( 'NONE',  ( 0.7071067811865486830, -0.7071067811865464625, -0.000000000000000000 ) ) ;
#1949=DIRECTION ( 'NONE',  ( -0.7071067811865486830, -0.7071067811865464625, 0.000000000000000000 ) ) ;
#1950=LINE ( 'NONE', #112210, #88812 ) ;
#1951=DIRECTION ( 'NONE',  ( 0.7071067811865486830, -0.7071067811865464625, -0.000000000000000000 ) ) ;
#1952=VERTEX_POINT ( 'NONE', #19358 ) ;
#1953=CARTESIAN_POINT ( 'NONE',  ( 22.49999999999985079, -5.947814304570765209, 5.000000000000000000 ) ) ;
#1954=LINE ( 'NONE', #24469, #134998 ) ;
#1955=LINE ( 'NONE', #13570, #50294 ) ;
#1957=EDGE_LOOP ( 'NONE', ( #112942, #63873, #141474, #33566 ) ) ;
#1958=ADVANCED_FACE ( 'NONE', ( #54864 ), #20773, .F. ) ;
#1960=ORIENTED_EDGE ( 'NONE', *, *, #30041, .F. ) ;
#1962=ORIENTED_EDGE ( 'NONE', *, *, #10892, .T. ) ;
#1963=FACE_OUTER_BOUND ( 'NONE', #11789, .T. ) ;
#1964=LINE ( 'NONE', #124513, #103480 ) ;
#1965=DIRECTION ( 'NONE',  ( -0.000000000000000000, 0.000000000000000000, 1.000000000000000000 ) ) ;
#1966=CARTESIAN_POINT ( 'NONE',  ( 2.999999999999988010, -12.41253812416062985, 4.000000000000000000 ) ) ;
#1967=ORIENTED_EDGE ( 'NONE', *, *, #36055, .T. ) ;
#1968=CARTESIAN_POINT ( 'NONE',  ( -3.489213562373097322, -27.52281430457057709, 5.000000000000000000 ) ) ;
#1969=CARTESIAN_POINT ( 'NONE',  ( -48.48921356237309510, -27.52281430457089328, 5.000000000000000000 ) ) ;
#1971=CARTESIAN_POINT ( 'NONE',  ( -29.20710678118634007, -17.24070752338410273, 5.000000000000000000 ) ) ;
#1973=ADVANCED_FACE ( 'NONE', ( #75889 ), #143273, .T. ) ;
#1974=VERTEX_POINT ( 'NONE', #32388 ) ;
#1975=CARTESIAN_POINT ( 'NONE',  ( 24.79333936457830134, 21.75929247661549226, 4.998822639870711626 ) ) ;
#1976=DIRECTION ( 'NONE',  ( 1.000000000000000000, 0.000000000000000000, 0.000000000000000000 ) ) ;
#1977=AXIS2_PLACEMENT_3D ( 'NONE', #134005, #102092, #34698 ) ;
#1978=AXIS2_PLACEMENT_3D ( 'NONE', #41884, #44027, #131034 ) ;
#1979=VECTOR ( 'NONE', #137755, 1000.000000000000000 ) ;
#1981=EDGE_LOOP ( 'NONE', ( #66680, #62829, #38339, #82103 ) ) ;
#1982=VECTOR ( 'NONE', #125447, 1000.000000000000000 ) ;
#1983=PLANE ( 'NONE',  #40026 ) ;
#1984=EDGE_CURVE ( 'NONE', #49245, #71694, #131696, .T. ) ;
#1987=CARTESIAN_POINT ( 'NONE',  ( 7.499999999999944045, -14.70932175296476352, -11.46312253303839057 ) ) ;
#1989=AXIS2_PLACEMENT_3D ( 'NONE', #93068, #48864, #122843 ) ;
#1994=EDGE_LOOP ( 'NONE', ( #80199, #136333, #15968, #43619 ) ) ;
#1995=ORIENTED_EDGE ( 'NONE', *, *, #47752, .F. ) ;
#1996=FACE_OUTER_BOUND ( 'NONE', #10193, .T. ) ;
#1997=ORIENTED_EDGE ( 'NONE', *, *, #45424, .F. ) ;
#2001=DIRECTION ( 'NONE',  ( 0.7071067811865486830, -0.7071067811865464625, -0.000000000000000000 ) ) ;
#2003=CARTESIAN_POINT ( 'NONE',  ( -15.18398860626900237, 28.73617430169797871, 5.000000000000000000 ) ) ;
#2004=DIRECTION ( 'NONE',  ( 0.7071067811865487940, 0.7071067811865463515, 0.000000000000000000 ) ) ;
#2005=DIRECTION ( 'NONE',  ( 0.000000000000000000, 0.000000000000000000, -1.000000000000000000 ) ) ;
#2007=VECTOR ( 'NONE', #69761, 1000.000000000000227 ) ;
#2008=AXIS2_PLACEMENT_3D ( 'NONE', #68547, #79451, #113432 ) ;
#2009=CARTESIAN_POINT ( 'NONE',  ( 10.49999999999992184, 21.43112307739196609, 4.000000000000000000 ) ) ;
#2010=ORIENTED_EDGE ( 'NONE', *, *, #87769, .F. ) ;
#2011=VECTOR ( 'NONE', #48325, 1000.000000000000000 ) ;
#2012=ADVANCED_FACE ( 'NONE', ( #20050 ), #43978, .F. ) ;
#2013=LINE ( 'NONE', #134755, #58046 ) ;
#2015=DIRECTION ( 'NONE',  ( -0.000000000000000000, 0.3543493200069153248, 0.9351131265310292928 ) ) ;
#2016=ORIENTED_EDGE ( 'NONE', *, *, #129111, .T. ) ;
#2018=ADVANCED_FACE ( 'NONE', ( #77352 ), #141119, .F. ) ;
#2019=ORIENTED_EDGE ( 'NONE', *, *, #9909, .T. ) ;
#2020=DIRECTION ( 'NONE',  ( -0.6830127018922181881, 0.6830127018922202975, -0.2588190451025214056 ) ) ;
#2021=ORIENTED_EDGE ( 'NONE', *, *, #76077, .T. ) ;
#2022=VERTEX_POINT ( 'NONE', #53411 ) ;
#2024=ORIENTED_EDGE ( 'NONE', *, *, #88951, .T. ) ;
#2025=VECTOR ( 'NONE', #59194, 1000.000000000000114 ) ;
#2026=EDGE_CURVE ( 'NONE', #86181, #127621, #31671, .T. ) ;
#2027=EDGE_CURVE ( 'NONE', #136233, #94607, #74475, .T. ) ;
#2029=CARTESIAN_POINT ( 'NONE',  ( -1.828169399223512848, -5.240707523384230626, 4.000000000000000000 ) ) ;
#2031=DIRECTION ( 'NONE',  ( 0.7071067811865487940, -0.7071067811865463515, 0.000000000000000000 ) ) ;
#2032=EDGE_CURVE ( 'NONE', #32915, #53582, #120054, .T. ) ;
#2034=PLANE ( 'NONE',  #79866 ) ;
#2036=CARTESIAN_POINT ( 'NONE',  ( -21.18398860626899349, 28.73617430169802134, 5.000000000000000000 ) ) ;
#2037=LINE ( 'NONE', #49180, #69913 ) ;
#2039=EDGE_CURVE ( 'NONE', #87384, #40271, #22888, .T. ) ;
#2040=CARTESIAN_POINT ( 'NONE',  ( -17.47599861414538580, 22.03583458319438293, 4.979811245910086726 ) ) ;
#2042=ADVANCED_FACE ( 'NONE', ( #89606 ), #114214, .F. ) ;
#2043=EDGE_LOOP ( 'NONE', ( #18243, #54537, #90165, #14547 ) ) ;
#2044=FACE_OUTER_BOUND ( 'NONE', #129847, .T. ) ;
#2045=LINE ( 'NONE', #124583, #121563 ) ;
#2046=DIRECTION ( 'NONE',  ( -0.7071067811865487940, -0.7071067811865463515, -0.000000000000000000 ) ) ;
#2047=VERTEX_POINT ( 'NONE', #59169 ) ;
#2048=EDGE_LOOP ( 'NONE', ( #59310, #107009, #82025, #89378 ) ) ;
#2051=LINE ( 'NONE', #77546, #93119 ) ;
#2052=FACE_OUTER_BOUND ( 'NONE', #89709, .T. ) ;
#2053=DIRECTION ( 'NONE',  ( -0.7071067811865487940, 0.7071067811865463515, -0.000000000000000000 ) ) ;
#2054=EDGE_CURVE ( 'NONE', #51885, #72728, #124382, .T. ) ;
#2055=CARTESIAN_POINT ( 'NONE',  ( 60.18398860626900415, 28.73617430169829490, 5.000000000000000000 ) ) ;
#2056=CARTESIAN_POINT ( 'NONE',  ( -19.42650926608379436, -2.782569431601979559, 4.369986656771231104 ) ) ;
#2057=ORIENTED_EDGE ( 'NONE', *, *, #35021, .F. ) ;
#2059=ORIENTED_EDGE ( 'NONE', *, *, #52310, .F. ) ;
#2060=EDGE_CURVE ( 'NONE', #104452, #81393, #3968, .T. ) ;
#2061=CARTESIAN_POINT ( 'NONE',  ( 51.48921356237309510, -27.52281430457091460, 5.000000000000000000 ) ) ;
#2066=FACE_OUTER_BOUND ( 'NONE', #85403, .T. ) ;
#2067=PLANE ( 'NONE',  #76647 ) ;
#2068=ORIENTED_EDGE ( 'NONE', *, *, #96696, .T. ) ;
#2071=CARTESIAN_POINT ( 'NONE',  ( 6.707106781186497280, 14.25929247661557575, 5.000000000000000000 ) ) ;
#2072=CARTESIAN_POINT ( 'NONE',  ( -33.29974487139158867, -27.71228299555229313, 4.000000000000000000 ) ) ;
#2073=DIRECTION ( 'NONE',  ( -0.000000000000000000, 0.3543493200069153248, 0.9351131265310292928 ) ) ;
#2074=DIRECTION ( 'NONE',  ( 0.7071067811865486830, -0.7071067811865464625, -0.000000000000000000 ) ) ;
#2075=ORIENTED_EDGE ( 'NONE', *, *, #99314, .T. ) ;
#2077=DIRECTION ( 'NONE',  ( -0.000000000000000000, 0.000000000000000000, 1.000000000000000000 ) ) ;
#2078=EDGE_CURVE ( 'NONE', #116493, #30958, #12037, .T. ) ;
#2079=VERTEX_POINT ( 'NONE', #112098 ) ;
#2080=VECTOR ( 'NONE', #49503, 1000.000000000000227 ) ;
#2081=AXIS2_PLACEMENT_3D ( 'NONE', #88011, #55400, #54686 ) ;
#2083=VECTOR ( 'NONE', #122169, 1000.000000000000000 ) ;
#2085=ORIENTED_EDGE ( 'NONE', *, *, #60241, .T. ) ;
#2086=ADVANCED_FACE ( 'NONE', ( #12745 ), #13448, .F. ) ;
#2087=ORIENTED_EDGE ( 'NONE', *, *, #73669, .T. ) ;
#2088=ORIENTED_EDGE ( 'NONE', *, *, #37606, .F. ) ;
#2089=DIRECTION ( 'NONE',  ( -0.3543493200069162685, -0.000000000000000000, -0.9351131265310288487 ) ) ;
#2090=CARTESIAN_POINT ( 'NONE',  ( -21.32816939922337340, -3.740707523384238176, 4.000000000000000000 ) ) ;
#2091=ORIENTED_EDGE ( 'NONE', *, *, #9525, .F. ) ;
#2094=ORIENTED_EDGE ( 'NONE', *, *, #29552, .T. ) ;
#2095=DIRECTION ( 'NONE',  ( -0.3543493200069162685, -0.000000000000000000, -0.9351131265310288487 ) ) ;
#2096=CARTESIAN_POINT ( 'NONE',  ( 34.92499999999998295, 22.22500000000000142, 4.000000000000000000 ) ) ;
#2097=CARTESIAN_POINT ( 'NONE',  ( 15.18398860626900237, 28.73617430169797871, 5.000000000000000000 ) ) ;
#2099=CARTESIAN_POINT ( 'NONE',  ( 15.65494483745372811, 5.259292476615665457, 12.77922209995897518 ) ) ;
#2100=EDGE_CURVE ( 'NONE', #105207, #47204, #122961, .T. ) ;
#2101=CARTESIAN_POINT ( 'NONE',  ( -15.70710678118642711, -3.740707523384238176, 5.000000000000000000 ) ) ;
#2102=LINE ( 'NONE', #46416, #125914 ) ;
#2107=LINE ( 'NONE', #705, #29778 ) ;
#2110=FACE_OUTER_BOUND ( 'NONE', #138548, .T. ) ;
#2111=ORIENTED_EDGE ( 'NONE', *, *, #119507, .F. ) ;
#2112=( BOUNDED_CURVE ( )  B_SPLINE_CURVE ( 3, ( #39492, #128628, #6795, #17692 ),
 .UNSPECIFIED., .F., .F. ) 
 B_SPLINE_CURVE_WITH_KNOTS ( ( 4, 4 ),
 ( 5.043186909253424055, 5.074607125596347856 ),
 .UNSPECIFIED. ) 
 CURVE ( )  GEOMETRIC_REPRESENTATION_ITEM ( )  RATIONAL_B_SPLINE_CURVE ( ( 1.000000000000000000, 0.9999177325257868620, 0.9999177325257868620, 1.000000000000000000 ) ) 
 REPRESENTATION_ITEM ( '' )  );
#2113=ORIENTED_EDGE ( 'NONE', *, *, #128807, .F. ) ;
#2115=ORIENTED_EDGE ( 'NONE', *, *, #36511, .F. ) ;
#2117=ORIENTED_EDGE ( 'NONE', *, *, #27601, .F. ) ;
#2118=DIRECTION ( 'NONE',  ( -0.3543493200069162685, -0.000000000000000000, -0.9351131265310288487 ) ) ;
#2119=DIRECTION ( 'NONE',  ( -0.6830127018922180770, -0.6830127018922204085, -0.2588190451025213501 ) ) ;
#2120=FACE_OUTER_BOUND ( 'NONE', #143010, .T. ) ;
#2121=EDGE_LOOP ( 'NONE', ( #45640, #4604, #130584, #5417 ) ) ;
#2123=DIRECTION ( 'NONE',  ( -0.6830127018922181881, 0.6830127018922202975, -0.2588190451025214056 ) ) ;
#2124=VECTOR ( 'NONE', #105539, 1000.000000000000227 ) ;
#2125=LINE ( 'NONE', #46438, #16321 ) ;
#2126=VECTOR ( 'NONE', #74739, 1000.000000000000000 ) ;
#2127=CARTESIAN_POINT ( 'NONE',  ( -39.48921356237310221, -27.52281430457082934, 5.000000000000000000 ) ) ;
#2128=CARTESIAN_POINT ( 'NONE',  ( 5.999999999999963585, -9.412538124160663600, 4.000000000000000000 ) ) ;
#2129=EDGE_CURVE ( 'NONE', #38121, #134952, #101194, .T. ) ;
#2130=PLANE ( 'NONE',  #97323 ) ;
#2131=VECTOR ( 'NONE', #120363, 999.9999999999998863 ) ;
#2132=CARTESIAN_POINT ( 'NONE',  ( 24.48921356237309510, -27.52281430457072631, 5.000000000000000000 ) ) ;
#2134=CARTESIAN_POINT ( 'NONE',  ( 34.42499999999998295, 22.22500000000000142, 5.000000000000000000 ) ) ;
#2135=VECTOR ( 'NONE', #53514, 1000.000000000000000 ) ;
#2136=CARTESIAN_POINT ( 'NONE',  ( 34.47516574401890921, 22.22311076525683760, 4.292435211492992231 ) ) ;
#2137=CARTESIAN_POINT ( 'NONE',  ( -12.70710678118644843, -15.74070752338412404, 5.000000000000000000 ) ) ;
#2138=DIRECTION ( 'NONE',  ( 0.7071067811865487940, 0.7071067811865463515, -0.000000000000000000 ) ) ;
#2142=ORIENTED_EDGE ( 'NONE', *, *, #125053, .F. ) ;
#2143=VERTEX_POINT ( 'NONE', #101914 ) ;
#2145=ORIENTED_EDGE ( 'NONE', *, *, #59090, .T. ) ;
#2146=EDGE_CURVE ( 'NONE', #142117, #54589, #2577, .T. ) ;
#2147=DIRECTION ( 'NONE',  ( 0.6830127018922180770, -0.6830127018922204085, -0.2588190451025213501 ) ) ;
#2149=CARTESIAN_POINT ( 'NONE',  ( 19.49999999999986500, -5.947814304570768762, 5.000000000000000000 ) ) ;
#2150=ADVANCED_FACE ( 'NONE', ( #26501 ), #16299, .F. ) ;
#2151=DIRECTION ( 'NONE',  ( 0.3543493200069162685, -0.000000000000000000, -0.9351131265310288487 ) ) ;
#2152=CARTESIAN_POINT ( 'NONE',  ( 11.51078643762690490, -27.52281430457047406, 5.000000000000000000 ) ) ;
#2155=EDGE_CURVE ( 'NONE', #8822, #119805, #59852, .T. ) ;
#2156=ORIENTED_EDGE ( 'NONE', *, *, #4066, .F. ) ;
#2157=VERTEX_POINT ( 'NONE', #114893 ) ;
#2159=DIRECTION ( 'NONE',  ( -0.000000000000000000, 0.000000000000000000, 1.000000000000000000 ) ) ;
#2160=ORIENTED_EDGE ( 'NONE', *, *, #20603, .F. ) ;
#2161=ORIENTED_EDGE ( 'NONE', *, *, #131259, .F. ) ;
#2163=DIRECTION ( 'NONE',  ( 0.7071067811865487940, 0.7071067811865463515, 0.000000000000000000 ) ) ;
#2164=ADVANCED_FACE ( 'NONE', ( #83028 ), #127218, .F. ) ;
#2166=CARTESIAN_POINT ( 'NONE',  ( 21.65295664585917379, -22.22500000000000142, 26.43950276819876422 ) ) ;
#2167=ORIENTED_EDGE ( 'NONE', *, *, #33107, .T. ) ;
#2169=CARTESIAN_POINT ( 'NONE',  ( 24.48921356237309510, -27.52281430457072631, 5.000000000000000000 ) ) ;
#2171=VERTEX_POINT ( 'NONE', #104767 ) ;
#2172=ORIENTED_EDGE ( 'NONE', *, *, #61266, .T. ) ;
#2173=CARTESIAN_POINT ( 'NONE',  ( 0.000000000000000000, -18.03360074219755660, 5.000000000000000000 ) ) ;
#2175=CARTESIAN_POINT ( 'NONE',  ( -34.42500000000001137, -21.72500000000000142, 0.000000000000000000 ) ) ;
#2176=ORIENTED_EDGE ( 'NONE', *, *, #117095, .T. ) ;
#2177=CARTESIAN_POINT ( 'NONE',  ( -5.816011393731002066, 28.73617430169783304, 5.000000000000000000 ) ) ;
#2178=EDGE_CURVE ( 'NONE', #89522, #15253, #138841, .T. ) ;
#2179=VECTOR ( 'NONE', #55374, 1000.000000000000000 ) ;
#2180=LINE ( 'NONE', #107924, #75697 ) ;
#2181=LINE ( 'NONE', #67519, #140887 ) ;
#2183=VECTOR ( 'NONE', #132936, 1000.000000000000000 ) ;
#2184=DIRECTION ( 'NONE',  ( 0.6830127018922180770, -0.6830127018922204085, -0.2588190451025213501 ) ) ;
#2185=VECTOR ( 'NONE', #103169, 1000.000000000000000 ) ;
#2186=FACE_BOUND ( 'NONE', #38740, .T. ) ;
#2187=VERTEX_POINT ( 'NONE', #7575 ) ;
#2188=PLANE ( 'NONE',  #6299 ) ;
#2189=CARTESIAN_POINT ( 'NONE',  ( -34.92500000000001137, -11.29530194282805233, 17.70209546082494256 ) ) ;
#2190=DIRECTION ( 'NONE',  ( -0.7071067811865486830, 0.7071067811865464625, 0.000000000000000000 ) ) ;
#2191=LINE ( 'NONE', #133477, #46278 ) ;
#2192=VERTEX_POINT ( 'NONE', #106897 ) ;
#2193=EDGE_LOOP ( 'NONE', ( #133761, #14164, #62737, #84970 ) ) ;
#2194=EDGE_LOOP ( 'NONE', ( #107474, #1633, #57374, #39206 ) ) ;
#2195=VECTOR ( 'NONE', #91323, 1000.000000000000000 ) ;
#2197=EDGE_CURVE ( 'NONE', #142484, #128301, #81620, .T. ) ;
#2199=VERTEX_POINT ( 'NONE', #125826 ) ;
#2200=VECTOR ( 'NONE', #10305, 1000.000000000000000 ) ;
#2201=CARTESIAN_POINT ( 'NONE',  ( -18.70710678118640757, 11.25929247661560417, 5.000000000000000000 ) ) ;
#2203=EDGE_CURVE ( 'NONE', #120482, #92375, #117057, .T. ) ;
#2204=PLANE ( 'NONE',  #10363 ) ;
#2205=ORIENTED_EDGE ( 'NONE', *, *, #38294, .F. ) ;
#2206=ADVANCED_FACE ( 'NONE', ( #28659 ), #73578, .F. ) ;
#2208=LINE ( 'NONE', #46528, #106041 ) ;
#2209=AXIS2_PLACEMENT_3D ( 'NONE', #126261, #115333, #72643 ) ;
#2210=VECTOR ( 'NONE', #32746, 999.9999999999998863 ) ;
#2211=EDGE_CURVE ( 'NONE', #139208, #22203, #126504, .T. ) ;
#2212=VECTOR ( 'NONE', #62111, 1000.000000000000000 ) ;
#2213=CARTESIAN_POINT ( 'NONE',  ( -22.36246187583885359, 22.22500000000000853, 4.000000000000000000 ) ) ;
#2214=FACE_OUTER_BOUND ( 'NONE', #130362, .T. ) ;
#2215=CARTESIAN_POINT ( 'NONE',  ( 0.000000000000000000, 0.000000000000000000, 5.000000000000000000 ) ) ;
#2216=CARTESIAN_POINT ( 'NONE',  ( -18.48921356237309510, -27.52281430457068367, 5.000000000000000000 ) ) ;
#2217=ADVANCED_FACE ( 'NONE', ( #115591 ), #62714, .F. ) ;
#2218=ORIENTED_EDGE ( 'NONE', *, *, #24523, .F. ) ;
#2220=ORIENTED_EDGE ( 'NONE', *, *, #140856, .T. ) ;
#2221=VERTEX_POINT ( 'NONE', #49708 ) ;
#2222=VECTOR ( 'NONE', #11802, 999.9999999999998863 ) ;
#2223=LINE ( 'NONE', #12414, #79795 ) ;
#2224=ORIENTED_EDGE ( 'NONE', *, *, #34832, .T. ) ;
#2225=VECTOR ( 'NONE', #93640, 999.9999999999998863 ) ;
#2226=VECTOR ( 'NONE', #69394, 999.9999999999998863 ) ;
#2227=ORIENTED_EDGE ( 'NONE', *, *, #117221, .T. ) ;
#2228=CARTESIAN_POINT ( 'NONE',  ( 2.206660635421510808, 21.75929247661549937, 4.998822639870701856 ) ) ;
#2229=ADVANCED_FACE ( 'NONE', ( #93885 ), #72192, .T. ) ;
#2230=ADVANCED_FACE ( 'NONE', ( #50402 ), #83767, .F. ) ;
#2231=VECTOR ( 'NONE', #8494, 1000.000000000000000 ) ;
#2232=CARTESIAN_POINT ( 'NONE',  ( -8.816011393731004731, 28.73617430169781173, 5.000000000000000000 ) ) ;
#2233=ORIENTED_EDGE ( 'NONE', *, *, #108014, .T. ) ;
#2234=VECTOR ( 'NONE', #63374, 999.9999999999998863 ) ;
#2235=CARTESIAN_POINT ( 'NONE',  ( 25.49999999999983658, 16.46639925780209879, 5.000000000000000000 ) ) ;
#2236=ADVANCED_FACE ( 'NONE', ( #30046 ), #130103, .F. ) ;
#2237=PLANE ( 'NONE',  #116146 ) ;
#2240=ORIENTED_EDGE ( 'NONE', *, *, #46303, .T. ) ;
#2242=LINE ( 'NONE', #124066, #103157 ) ;
#2243=LINE ( 'NONE', #45814, #111387 ) ;
#2247=VECTOR ( 'NONE', #39055, 1000.000000000000000 ) ;
#2248=CARTESIAN_POINT ( 'NONE',  ( 75.48921356237309510, -27.52281430457107803, 5.000000000000000000 ) ) ;
#2249=VERTEX_POINT ( 'NONE', #130835 ) ;
#2250=LINE ( 'NONE', #18116, #81105 ) ;
#2251=ORIENTED_EDGE ( 'NONE', *, *, #133996, .T. ) ;
#2252=DIRECTION ( 'NONE',  ( 0.6830127018922180770, -0.6830127018922204085, -0.2588190451025213501 ) ) ;
#2253=CARTESIAN_POINT ( 'NONE',  ( 31.77149322861315994, 20.25929247661551003, 7.808871592221842128 ) ) ;
#2254=CARTESIAN_POINT ( 'NONE',  ( -36.48921356237310221, -27.52281430457080802, 5.000000000000000000 ) ) ;
#2255=VERTEX_POINT ( 'NONE', #75720 ) ;
#2257=DIRECTION ( 'NONE',  ( -0.7071067811865486830, -0.7071067811865464625, 0.000000000000000000 ) ) ;
#2258=EDGE_CURVE ( 'NONE', #69590, #123136, #53990, .T. ) ;
#2259=ORIENTED_EDGE ( 'NONE', *, *, #121085, .F. ) ;
#2260=AXIS2_PLACEMENT_3D ( 'NONE', #100342, #58316, #77187 ) ;
#2261=CARTESIAN_POINT ( 'NONE',  ( -17.99999999999987210, -16.06887692260766087, 4.000000000000000000 ) ) ;
#2262=VERTEX_POINT ( 'NONE', #10434 ) ;
#2263=DIRECTION ( 'NONE',  ( -1.000000000000000000, 0.000000000000000000, 0.000000000000000000 ) ) ;
#2264=DIRECTION ( 'NONE',  ( 0.7071067811865487940, 0.7071067811865463515, 0.000000000000000000 ) ) ;
#2265=VERTEX_POINT ( 'NONE', #131523 ) ;
#2266=ORIENTED_EDGE ( 'NONE', *, *, #58497, .T. ) ;
#2268=CARTESIAN_POINT ( 'NONE',  ( -26.99999999999981526, 13.93112307739204425, 4.000000000000000000 ) ) ;
#2269=ORIENTED_EDGE ( 'NONE', *, *, #83811, .F. ) ;
#2270=EDGE_CURVE ( 'NONE', #47602, #60604, #19188, .T. ) ;
#2271=LINE ( 'NONE', #115133, #96914 ) ;
#2274=CARTESIAN_POINT ( 'NONE',  ( -0.3281693992235245605, -12.74070752338415424, 4.000000000000000000 ) ) ;
#2276=LINE ( 'NONE', #100910, #93038 ) ;
#2277=LINE ( 'NONE', #11738, #84123 ) ;
#2280=DIRECTION ( 'NONE',  ( -0.000000000000000000, 0.000000000000000000, 1.000000000000000000 ) ) ;
#2281=ORIENTED_EDGE ( 'NONE', *, *, #4826, .T. ) ;
#2282=EDGE_LOOP ( 'NONE', ( #51623, #89592, #38507, #68224 ) ) ;
#2283=ORIENTED_EDGE ( 'NONE', *, *, #74281, .T. ) ;
#2285=VECTOR ( 'NONE', #134611, 999.9999999999998863 ) ;
#2286=EDGE_LOOP ( 'NONE', ( #137657, #83804, #58420, #112384 ) ) ;
#2288=EDGE_CURVE ( 'NONE', #127030, #77873, #120613, .T. ) ;
#2289=ORIENTED_EDGE ( 'NONE', *, *, #659, .T. ) ;
#2292=LINE ( 'NONE', #45867, #136560 ) ;
#2293=VECTOR ( 'NONE', #82016, 1000.000000000000227 ) ;
#2294=AXIS2_PLACEMENT_3D ( 'NONE', #108004, #40656, #97118 ) ;
#2296=VERTEX_POINT ( 'NONE', #54689 ) ;
#2297=CARTESIAN_POINT ( 'NONE',  ( 25.49999999999981881, -8.568876922607733704, 4.000000000000000000 ) ) ;
#2298=DIRECTION ( 'NONE',  ( -0.7071067811865487940, 0.7071067811865463515, -0.000000000000000000 ) ) ;
#2300=CARTESIAN_POINT ( 'NONE',  ( 31.82816939922330235, -11.24070752338417201, 4.000000000000000000 ) ) ;
#2301=CARTESIAN_POINT ( 'NONE',  ( -48.29974487139158867, -27.71228299555239971, 4.000000000000000000 ) ) ;
#2303=ADVANCED_FACE ( 'NONE', ( #19883 ), #8273, .F. ) ;
#2304=ORIENTED_EDGE ( 'NONE', *, *, #24463, .F. ) ;
#2305=CARTESIAN_POINT ( 'NONE',  ( -22.49999999999984013, 1.030536316426494681, -5.498701923753746001 ) ) ;
#2306=DIRECTION ( 'NONE',  ( 0.7071067811865487940, 0.7071067811865463515, 0.000000000000000000 ) ) ;
#2307=CARTESIAN_POINT ( 'NONE',  ( -60.18398860626900415, 28.73617430169829490, 5.000000000000000000 ) ) ;
#2308=VECTOR ( 'NONE', #136055, 1000.000000000000227 ) ;
#2310=PLANE ( 'NONE',  #119253 ) ;
#2313=CARTESIAN_POINT ( 'NONE',  ( 7.499999999999947597, 8.900465351122155866, -2.516491619111531186 ) ) ;
#2315=DIRECTION ( 'NONE',  ( -0.7071067811865486830, -0.7071067811865464625, 0.000000000000000000 ) ) ;
#2316=LINE ( 'NONE', #99495, #108601 ) ;
#2318=VERTEX_POINT ( 'NONE', #30800 ) ;
#2321=FACE_OUTER_BOUND ( 'NONE', #6003, .T. ) ;
#2322=VECTOR ( 'NONE', #61577, 1000.000000000000000 ) ;
#2323=ORIENTED_EDGE ( 'NONE', *, *, #40337, .F. ) ;
#2324=DIRECTION ( 'NONE',  ( 0.7071067811865487940, 0.7071067811865463515, 0.000000000000000000 ) ) ;
#2325=CARTESIAN_POINT ( 'NONE',  ( -34.92500000000001137, 9.662461875838888048, 4.000000000000000000 ) ) ;
#2327=AXIS2_PLACEMENT_3D ( 'NONE', #38047, #27143, #138787 ) ;
#2329=EDGE_CURVE ( 'NONE', #73005, #76116, #75028, .T. ) ;
#2330=ORIENTED_EDGE ( 'NONE', *, *, #12806, .F. ) ;
#2331=VECTOR ( 'NONE', #30888, 1000.000000000000000 ) ;
#2332=CARTESIAN_POINT ( 'NONE',  ( 18.29974487139159223, -27.71228299555219010, 4.000000000000000000 ) ) ;
#2333=ORIENTED_EDGE ( 'NONE', *, *, #39966, .F. ) ;
#2334=CARTESIAN_POINT ( 'NONE',  ( 4.499999999999976019, -1.912538124160739095, 4.000000000000000000 ) ) ;
#2335=AXIS2_PLACEMENT_3D ( 'NONE', #45709, #2123, #90624 ) ;
#2336=CARTESIAN_POINT ( 'NONE',  ( 59.99451991528749772, 28.92564299267980132, 4.000000000000000000 ) ) ;
#2337=LINE ( 'NONE', #43735, #60646 ) ;
#2338=PLANE ( 'NONE',  #113590 ) ;
#2339=ORIENTED_EDGE ( 'NONE', *, *, #116323, .T. ) ;
#2340=ADVANCED_FACE ( 'NONE', ( #64128 ), #108293, .F. ) ;
#2341=LINE ( 'NONE', #12526, #72047 ) ;
#2343=VECTOR ( 'NONE', #117115, 1000.000000000000227 ) ;
#2345=EDGE_CURVE ( 'NONE', #63317, #74837, #43800, .T. ) ;
#2346=CARTESIAN_POINT ( 'NONE',  ( -27.29974487139158512, -27.71228299555225405, 4.000000000000000000 ) ) ;
#2348=FACE_OUTER_BOUND ( 'NONE', #113078, .T. ) ;
#2349=CARTESIAN_POINT ( 'NONE',  ( 21.48921356237309155, -27.52281430457070499, 5.000000000000000000 ) ) ;
#2350=AXIS2_PLACEMENT_3D ( 'NONE', #72169, #81599, #114193 ) ;
#2354=FACE_OUTER_BOUND ( 'NONE', #128403, .T. ) ;
#2355=CARTESIAN_POINT ( 'NONE',  ( 34.45011844616453800, 7.516280811637427561, 5.000000000000001776 ) ) ;
#2356=ORIENTED_EDGE ( 'NONE', *, *, #58952, .F. ) ;
#2357=ORIENTED_EDGE ( 'NONE', *, *, #102896, .T. ) ;
#2358=AXIS2_PLACEMENT_3D ( 'NONE', #52422, #95217, #41545 ) ;
#2360=ORIENTED_EDGE ( 'NONE', *, *, #25504, .T. ) ;
#2361=EDGE_CURVE ( 'NONE', #22428, #43234, #56862, .T. ) ;
#2363=VERTEX_POINT ( 'NONE', #102482 ) ;
#2364=CARTESIAN_POINT ( 'NONE',  ( 34.92499999999998295, 7.701930566820908375, 4.500000000000000888 ) ) ;
#2365=VECTOR ( 'NONE', #142092, 1000.000000000000000 ) ;
#2366=DIRECTION ( 'NONE',  ( 0.7071067811865487940, 0.7071067811865463515, 0.000000000000000000 ) ) ;
#2367=FACE_BOUND ( 'NONE', #6822, .T. ) ;
#2368=CARTESIAN_POINT ( 'NONE',  ( -2.999999999999978240, -10.06887692260771416, 4.000000000000000000 ) ) ;
#2369=DIRECTION ( 'NONE',  ( -0.6830127018922180770, -0.6830127018922204085, -0.2588190451025213501 ) ) ;
#2370=DIRECTION ( 'NONE',  ( -0.3543493200069162685, -0.000000000000000000, -0.9351131265310288487 ) ) ;
#2372=ORIENTED_EDGE ( 'NONE', *, *, #50186, .F. ) ;
#2373=VECTOR ( 'NONE', #127306, 999.9999999999998863 ) ;
#2374=ORIENTED_EDGE ( 'NONE', *, *, #73069, .F. ) ;
#2375=CARTESIAN_POINT ( 'NONE',  ( -54.18398860626899705, 28.73617430169825226, 5.000000000000000000 ) ) ;
#2376=ORIENTED_EDGE ( 'NONE', *, *, #4143, .T. ) ;
#2377=ADVANCED_FACE ( 'NONE', ( #3131 ), #91585, .F. ) ;
#2378=ADVANCED_FACE ( 'NONE', ( #44553 ), #77858, .F. ) ;
#2379=ORIENTED_EDGE ( 'NONE', *, *, #58155, .T. ) ;
#2382=DIRECTION ( 'NONE',  ( 0.7071067811865486830, -0.7071067811865464625, -0.000000000000000000 ) ) ;
#2384=EDGE_LOOP ( 'NONE', ( #79358, #5147, #58635, #32402 ) ) ;
#2385=DIRECTION ( 'NONE',  ( 0.7071067811865487940, -0.7071067811865463515, 0.000000000000000000 ) ) ;
#2386=VECTOR ( 'NONE', #76252, 1000.000000000000000 ) ;
#2387=EDGE_CURVE ( 'NONE', #133793, #49119, #123531, .T. ) ;
#2388=ADVANCED_FACE ( 'NONE', ( #35812 ), #24194, .F. ) ;
#2389=LINE ( 'NONE', #135801, #12501 ) ;
#2390=VECTOR ( 'NONE', #68776, 1000.000000000000227 ) ;
#2392=PLANE ( 'NONE',  #80277 ) ;
#2393=CARTESIAN_POINT ( 'NONE',  ( -34.49999999999975842, 10.46425560840038038, 4.994342998332163219 ) ) ;
#2396=CARTESIAN_POINT ( 'NONE',  ( 1.828169399223514624, -2.240707523384266153, 4.000000000000000000 ) ) ;
#2397=DIRECTION ( 'NONE',  ( 0.6830127018922180770, -0.6830127018922204085, -0.2588190451025213501 ) ) ;
#2398=VERTEX_POINT ( 'NONE', #111923 ) ;
#2399=VECTOR ( 'NONE', #22392, 1000.000000000000227 ) ;
#2400=AXIS2_PLACEMENT_3D ( 'NONE', #73798, #54226, #31026 ) ;
#2402=VECTOR ( 'NONE', #87077, 1000.000000000000227 ) ;
#2403=LINE ( 'NONE', #34357, #102928 ) ;
#2404=CARTESIAN_POINT ( 'NONE',  ( 20.28242261357419096, -21.73023691814493930, 5.000000000000000888 ) ) ;
#2405=ORIENTED_EDGE ( 'NONE', *, *, #73426, .F. ) ;
#2407=ORIENTED_EDGE ( 'NONE', *, *, #53785, .T. ) ;
#2408=ORIENTED_EDGE ( 'NONE', *, *, #48236, .T. ) ;
#2409=LINE ( 'NONE', #137251, #24402 ) ;
#2410=EDGE_CURVE ( 'NONE', #8692, #92047, #6079, .T. ) ;
#2411=ADVANCED_FACE ( 'NONE', ( #69137 ), #41291, .F. ) ;
#2415=CARTESIAN_POINT ( 'NONE',  ( -16.49999999999988631, -12.66682484999667757, -0.6294897503864330668 ) ) ;
#2419=ORIENTED_EDGE ( 'NONE', *, *, #68952, .T. ) ;
#2420=DIRECTION ( 'NONE',  ( -0.7071067811865486830, -0.7071067811865464625, 0.000000000000000000 ) ) ;
#2422=VECTOR ( 'NONE', #64920, 1000.000000000000000 ) ;
#2423=CARTESIAN_POINT ( 'NONE',  ( -77.99451991528749772, 28.92564299267992567, 4.000000000000000000 ) ) ;
#2424=EDGE_CURVE ( 'NONE', #31384, #17080, #17401, .T. ) ;
#2425=LINE ( 'NONE', #91610, #7713 ) ;
#2427=VERTEX_POINT ( 'NONE', #84810 ) ;
#2428=DIRECTION ( 'NONE',  ( -0.7071067811865486830, -0.7071067811865464625, 0.000000000000000000 ) ) ;
#2429=CARTESIAN_POINT ( 'NONE',  ( 17.99999999999986855, -22.22500000000000142, 4.412002311790053533 ) ) ;
#2430=DIRECTION ( 'NONE',  ( -0.6830127018922181881, 0.6830127018922202975, -0.2588190451025214056 ) ) ;
#2431=ORIENTED_EDGE ( 'NONE', *, *, #21887, .T. ) ;
#2432=VECTOR ( 'NONE', #42719, 1000.000000000000227 ) ;
#2433=PLANE ( 'NONE',  #73651 ) ;
#2434=LINE ( 'NONE', #80068, #52573 ) ;
#2435=VECTOR ( 'NONE', #64655, 1000.000000000000227 ) ;
#2437=LINE ( 'NONE', #47455, #42573 ) ;
#2438=CARTESIAN_POINT ( 'NONE',  ( 39.48921356237310221, -27.52281430457082934, 5.000000000000000000 ) ) ;
#2439=DIRECTION ( 'NONE',  ( -0.3543493200069162685, -0.000000000000000000, -0.9351131265310288487 ) ) ;
#2440=ADVANCED_FACE ( 'NONE', ( #5787 ), #100695, .F. ) ;
#2441=CARTESIAN_POINT ( 'NONE',  ( -34.92500000000001137, 22.22500000000000142, 4.000000000000000000 ) ) ;
#2442=VECTOR ( 'NONE', #53297, 1000.000000000000000 ) ;
#2445=DIRECTION ( 'NONE',  ( 0.7071067811865486830, -0.7071067811865464625, -0.000000000000000000 ) ) ;
#2446=CARTESIAN_POINT ( 'NONE',  ( -2.999999999999981792, 1.761378380278681099, -6.096875308897261370 ) ) ;
#2447=ORIENTED_EDGE ( 'NONE', *, *, #78535, .T. ) ;
#2448=AXIS2_PLACEMENT_3D ( 'NONE', #64910, #54750, #119948 ) ;
#2450=ORIENTED_EDGE ( 'NONE', *, *, #137199, .T. ) ;
#2451=EDGE_CURVE ( 'NONE', #142117, #1085, #9341, .T. ) ;
#2452=CARTESIAN_POINT ( 'NONE',  ( 72.48921356237309510, -27.52281430457106026, 5.000000000000000000 ) ) ;
#2453=CARTESIAN_POINT ( 'NONE',  ( -20.99451991528748707, 28.92564299267952777, 4.000000000000000000 ) ) ;
#2456=DIRECTION ( 'NONE',  ( 0.3543493200069162685, -0.000000000000000000, -0.9351131265310288487 ) ) ;
#2457=CARTESIAN_POINT ( 'NONE',  ( -9.183988606268997046, 28.73617430169793607, 5.000000000000000000 ) ) ;
#2458=DIRECTION ( 'NONE',  ( 0.7071067811865487940, 0.7071067811865463515, -0.000000000000000000 ) ) ;
#2460=CARTESIAN_POINT ( 'NONE',  ( -14.70025512860841133, -27.71228299555195917, 4.000000000000000000 ) ) ;
#2462=AXIS2_PLACEMENT_3D ( 'NONE', #6569, #71916, #105215 ) ;
#2463=DIRECTION ( 'NONE',  ( 0.7071067811865487940, 0.7071067811865463515, 0.000000000000000000 ) ) ;
#2464=CARTESIAN_POINT ( 'NONE',  ( 18.18398860626898994, 28.73617430169800002, 5.000000000000000000 ) ) ;
#2467=DIRECTION ( 'NONE',  ( -0.7071067811865486830, 0.7071067811865463515, 0.000000000000000000 ) ) ;
#2468=LINE ( 'NONE', #116785, #78926 ) ;
#2469=ORIENTED_EDGE ( 'NONE', *, *, #5476, .T. ) ;
#2471=ORIENTED_EDGE ( 'NONE', *, *, #87263, .F. ) ;
#2472=DIRECTION ( 'NONE',  ( -0.7071067811865486830, -0.7071067811865464625, -0.000000000000000000 ) ) ;
#2474=DIRECTION ( 'NONE',  ( -0.000000000000000000, -0.3543493200069152693, 0.9351131265310292928 ) ) ;
#2475=PLANE ( 'NONE',  #37052 ) ;
#2476=CARTESIAN_POINT ( 'NONE',  ( 17.24139925780192328, 21.72500000000000142, 5.000000000000000000 ) ) ;
#2477=DIRECTION ( 'NONE',  ( -0.7071067811865487940, 0.7071067811865463515, 0.000000000000000000 ) ) ;
#2480=CARTESIAN_POINT ( 'NONE',  ( -8.999999999999944933, -13.39766691384885000, -10.96608748226463703 ) ) ;
#2485=CARTESIAN_POINT ( 'NONE',  ( -3.183988606268992161, 28.73617430169789699, 5.000000000000000000 ) ) ;
#2487=DIRECTION ( 'NONE',  ( -0.000000000000000000, 0.3543493200069153248, 0.9351131265310292928 ) ) ;
#2488=CARTESIAN_POINT ( 'NONE',  ( -48.29974487139158867, -27.71228299555239971, 4.000000000000000000 ) ) ;
#2491=DIRECTION ( 'NONE',  ( -0.7071067811865487940, 0.7071067811865463515, -0.000000000000000000 ) ) ;
#2492=DIRECTION ( 'NONE',  ( 0.7071067811865486830, -0.7071067811865464625, -0.000000000000000000 ) ) ;
#2493=ADVANCED_FACE ( 'NONE', ( #112288 ), #12937, .F. ) ;
#2494=CARTESIAN_POINT ( 'NONE',  ( 25.49999999999982236, -6.839392718269110105, -8.480912228396146446 ) ) ;
#2495=ORIENTED_EDGE ( 'NONE', *, *, #54161, .T. ) ;
#2496=AXIS2_PLACEMENT_3D ( 'NONE', #131929, #20996, #21729 ) ;
#2497=FACE_OUTER_BOUND ( 'NONE', #13532, .T. ) ;
#2502=CARTESIAN_POINT ( 'NONE',  ( 22.49999999999984013, -13.91253812416061031, 4.000000000000000000 ) ) ;
#2503=ORIENTED_EDGE ( 'NONE', *, *, #8740, .T. ) ;
#2505=ORIENTED_EDGE ( 'NONE', *, *, #68906, .F. ) ;
#2506=VECTOR ( 'NONE', #105374, 1000.000000000000000 ) ;
#2507=AXIS2_PLACEMENT_3D ( 'NONE', #72961, #96077, #117116 ) ;
#2508=VECTOR ( 'NONE', #461, 1000.000000000000000 ) ;
#2509=CARTESIAN_POINT ( 'NONE',  ( -23.99999999999982592, -0.4125381241607464222, 4.000000000000000000 ) ) ;
#2510=DIRECTION ( 'NONE',  ( -0.6830127018922181881, 0.6830127018922202975, -0.2588190451025214056 ) ) ;
#2511=CARTESIAN_POINT ( 'NONE',  ( -13.08638746355377158, 2.894607053745204883, 4.324337194087686242 ) ) ;
#2512=EDGE_CURVE ( 'NONE', #77572, #132198, #50582, .T. ) ;
#2513=DIRECTION ( 'NONE',  ( -0.6830127018922181881, 0.6830127018922202975, -0.2588190451025214056 ) ) ;
#2515=EDGE_LOOP ( 'NONE', ( #29956, #713, #35393, #126362 ) ) ;
#2516=EDGE_CURVE ( 'NONE', #110269, #57315, #124577, .T. ) ;
#2517=LINE ( 'NONE', #48199, #108607 ) ;
#2519=DIRECTION ( 'NONE',  ( 0.6830127018922180770, -0.6830127018922204085, -0.2588190451025213501 ) ) ;
#2521=DIRECTION ( 'NONE',  ( 0.3543493200069162685, -0.000000000000000000, -0.9351131265310288487 ) ) ;
#2522=ORIENTED_EDGE ( 'NONE', *, *, #75026, .T. ) ;
#2523=ORIENTED_EDGE ( 'NONE', *, *, #142075, .F. ) ;
#2525=ORIENTED_EDGE ( 'NONE', *, *, #62158, .T. ) ;
#2526=EDGE_CURVE ( 'NONE', #91761, #87588, #2037, .T. ) ;
#2527=VECTOR ( 'NONE', #35963, 999.9999999999998863 ) ;
#2528=CARTESIAN_POINT ( 'NONE',  ( 27.70710678118635784, -15.74070752338411694, 5.000000000000000000 ) ) ;
#2529=CARTESIAN_POINT ( 'NONE',  ( -26.99451991528749417, 28.92564299267956685, 4.000000000000000000 ) ) ;
#2530=CARTESIAN_POINT ( 'NONE',  ( 44.99451991528749772, 28.92564299267969474, 4.000000000000000000 ) ) ;
#2532=CARTESIAN_POINT ( 'NONE',  ( 19.83957586139685247, 9.091547215995101183, 4.000000000000000000 ) ) ;
#2533=DIRECTION ( 'NONE',  ( -0.000000000000000000, 0.3543493200069153248, 0.9351131265310292928 ) ) ;
#2534=ORIENTED_EDGE ( 'NONE', *, *, #72740, .F. ) ;
#2536=DIRECTION ( 'NONE',  ( 0.7071067811865487940, -0.7071067811865463515, 0.000000000000000000 ) ) ;
#2538=EDGE_CURVE ( 'NONE', #133870, #105072, #90532, .T. ) ;
#2540=ORIENTED_EDGE ( 'NONE', *, *, #52332, .T. ) ;
#2541=VECTOR ( 'NONE', #87249, 1000.000000000000000 ) ;
#2542=LINE ( 'NONE', #14864, #102349 ) ;
#2545=DIRECTION ( 'NONE',  ( 1.000000000000000000, 0.000000000000000000, 0.000000000000000000 ) ) ;
#2546=EDGE_CURVE ( 'NONE', #109916, #119711, #4149, .T. ) ;
#2548=EDGE_LOOP ( 'NONE', ( #1662, #92443, #50337, #60677 ) ) ;
#2549=FACE_BOUND ( 'NONE', #124058, .T. ) ;
#2550=AXIS2_PLACEMENT_3D ( 'NONE', #133394, #68175, #134839 ) ;
#2551=CARTESIAN_POINT ( 'NONE',  ( -5.816011393731002066, 28.73617430169783304, 5.000000000000000000 ) ) ;
#2552=PLANE ( 'NONE',  #55951 ) ;
#2555=PLANE ( 'NONE',  #35011 ) ;
#2559=VERTEX_POINT ( 'NONE', #70932 ) ;
#2561=ORIENTED_EDGE ( 'NONE', *, *, #49898, .T. ) ;
#2562=PLANE ( 'NONE',  #120600 ) ;
#2563=EDGE_LOOP ( 'NONE', ( #129844, #42649, #110459, #102078 ) ) ;
#2564=ADVANCED_FACE ( 'NONE', ( #115083 ), #37583, .F. ) ;
#2565=VECTOR ( 'NONE', #11236, 1000.000000000000000 ) ;
#2566=LINE ( 'NONE', #35254, #47052 ) ;
#2567=VECTOR ( 'NONE', #109992, 1000.000000000000227 ) ;
#2568=LINE ( 'NONE', #101185, #98768 ) ;
#2570=EDGE_CURVE ( 'NONE', #58171, #58911, #81089, .T. ) ;
#2571=DIRECTION ( 'NONE',  ( -0.7071067811865486830, 0.7071067811865464625, 0.000000000000000000 ) ) ;
#2573=DIRECTION ( 'NONE',  ( -0.000000000000000000, 0.3543493200069153248, 0.9351131265310292928 ) ) ;
#2574=CARTESIAN_POINT ( 'NONE',  ( -6.489213562373093325, -27.52281430457059841, 5.000000000000000000 ) ) ;
#2575=CARTESIAN_POINT ( 'NONE',  ( 27.18398860626900060, 28.73617430169806042, 5.000000000000000000 ) ) ;
#2576=DIRECTION ( 'NONE',  ( 0.7071067811865487940, 0.7071067811865463515, 0.000000000000000000 ) ) ;
#2577=LINE ( 'NONE', #15571, #54362 ) ;
#2578=CARTESIAN_POINT ( 'NONE',  ( 17.11087965568911073, 8.820243421702873121, 4.000000000000000000 ) ) ;
#2579=VECTOR ( 'NONE', #72608, 999.9999999999998863 ) ;
#2580=CARTESIAN_POINT ( 'NONE',  ( 19.98012225071440895, -17.24070752338409562, 20.23474786156473826 ) ) ;
#2583=CARTESIAN_POINT ( 'NONE',  ( 15.29974487139158867, -27.71228299555216879, 4.000000000000000000 ) ) ;
#2584=( BOUNDED_CURVE ( )  B_SPLINE_CURVE ( 3, ( #9499, #75515, #30595, #76227 ),
 .UNSPECIFIED., .F., .T. ) 
 B_SPLINE_CURVE_WITH_KNOTS ( ( 4, 4 ),
 ( 4.350170835173025274, 4.500739107949216056 ),
 .UNSPECIFIED. ) 
 CURVE ( )  GEOMETRIC_REPRESENTATION_ITEM ( )  RATIONAL_B_SPLINE_CURVE ( ( 1.000000000000000000, 0.9981116584018956406, 0.9981116584018956406, 1.000000000000000000 ) ) 
 REPRESENTATION_ITEM ( '' )  );
#2586=ORIENTED_EDGE ( 'NONE', *, *, #79397, .F. ) ;
#2587=VERTEX_POINT ( 'NONE', #92637 ) ;
#2588=ADVANCED_FACE ( 'NONE', ( #60051 ), #4884, .F. ) ;
#2589=EDGE_CURVE ( 'NONE', #29676, #23874, #102839, .T. ) ;
#2590=ORIENTED_EDGE ( 'NONE', *, *, #71794, .T. ) ;
#2592=VECTOR ( 'NONE', #112371, 1000.000000000000114 ) ;
#2593=ORIENTED_EDGE ( 'NONE', *, *, #55401, .T. ) ;
#2596=LINE ( 'NONE', #44752, #65693 ) ;
#2597=ADVANCED_FACE ( 'NONE', ( #39733 ), #73761, .F. ) ;
#2600=ORIENTED_EDGE ( 'NONE', *, *, #59293, .F. ) ;
#2601=LINE ( 'NONE', #35994, #58058 ) ;
#2602=VECTOR ( 'NONE', #38318, 1000.000000000000227 ) ;
#2603=ADVANCED_FACE ( 'NONE', ( #8454 ), #71635, .F. ) ;
#2604=FACE_OUTER_BOUND ( 'NONE', #55083, .T. ) ;
#2605=ORIENTED_EDGE ( 'NONE', *, *, #23899, .T. ) ;
#2607=DIRECTION ( 'NONE',  ( 0.6830127018922181881, 0.6830127018922202975, -0.2588190451025214056 ) ) ;
#2610=AXIS2_PLACEMENT_3D ( 'NONE', #62691, #37360, #72166 ) ;
#2611=ORIENTED_EDGE ( 'NONE', *, *, #44892, .T. ) ;
#2612=CARTESIAN_POINT ( 'NONE',  ( -14.99451991528749595, 28.92564299267948513, 4.000000000000000000 ) ) ;
#2614=ORIENTED_EDGE ( 'NONE', *, *, #58952, .T. ) ;
#2615=ORIENTED_EDGE ( 'NONE', *, *, #20892, .F. ) ;
#2616=LINE ( 'NONE', #58509, #63282 ) ;
#2617=AXIS2_PLACEMENT_3D ( 'NONE', #3517, #16545, #83257 ) ;
#2618=VECTOR ( 'NONE', #104119, 1000.000000000000000 ) ;
#2619=VECTOR ( 'NONE', #15874, 1000.000000000000000 ) ;
#2620=CIRCLE ( 'NONE', #223, 5.968999999999998529 ) ;
#2622=CARTESIAN_POINT ( 'NONE',  ( 7.499999999999951150, -2.947814304570795851, 5.000000000000000000 ) ) ;
#2623=LINE ( 'NONE', #62757, #83360 ) ;
#2624=LINE ( 'NONE', #25821, #185 ) ;
#2626=ORIENTED_EDGE ( 'NONE', *, *, #1398, .T. ) ;
#2628=EDGE_CURVE ( 'NONE', #100474, #12218, #16500, .T. ) ;
#2629=ADVANCED_FACE ( 'NONE', ( #49896 ), #94071, .T. ) ;
#2631=LINE ( 'NONE', #80942, #120257 ) ;
#2632=CARTESIAN_POINT ( 'NONE',  ( -23.54739889332687497, 7.099584588756134629, 5.000000000000000000 ) ) ;
#2633=VECTOR ( 'NONE', #118826, 1000.000000000000000 ) ;
#2634=CARTESIAN_POINT ( 'NONE',  ( -28.49999999999980105, 6.277155672890246230, -3.510561720658876173 ) ) ;
#2635=VERTEX_POINT ( 'NONE', #117937 ) ;
#2636=ORIENTED_EDGE ( 'NONE', *, *, #130554, .T. ) ;
#2637=ORIENTED_EDGE ( 'NONE', *, *, #76318, .T. ) ;
#2638=CARTESIAN_POINT ( 'NONE',  ( 34.49999999999975842, -20.53675388469227769, 2.352720554255973706 ) ) ;
#2639=CARTESIAN_POINT ( 'NONE',  ( -32.99999999999976552, -15.03360074219758502, 5.000000000000000000 ) ) ;
#2641=CARTESIAN_POINT ( 'NONE',  ( 42.29974487139158157, -27.71228299555235708, 4.000000000000000000 ) ) ;
#2643=VECTOR ( 'NONE', #79119, 1000.000000000000000 ) ;
#2644=VECTOR ( 'NONE', #53378, 1000.000000000000000 ) ;
#2645=DIRECTION ( 'NONE',  ( -0.000000000000000000, 0.3543493200069153248, 0.9351131265310292928 ) ) ;
#2647=LINE ( 'NONE', #103384, #90379 ) ;
#2648=LINE ( 'NONE', #84369, #69805 ) ;
#2649=CARTESIAN_POINT ( 'NONE',  ( -45.29974487139158867, -27.71228299555237840, 4.000000000000000000 ) ) ;
#2650=ORIENTED_EDGE ( 'NONE', *, *, #46020, .F. ) ;
#2652=AXIS2_PLACEMENT_3D ( 'NONE', #81164, #113040, #71008 ) ;
#2653=VERTEX_POINT ( 'NONE', #72384 ) ;
#2655=CARTESIAN_POINT ( 'NONE',  ( -8.999999999999932498, 20.96639925780204905, 5.000000000000000000 ) ) ;
#2656=ORIENTED_EDGE ( 'NONE', *, *, #78074, .F. ) ;
#2657=VECTOR ( 'NONE', #90231, 1000.000000000000000 ) ;
#2658=DIRECTION ( 'NONE',  ( 0.7071067811865487940, 0.7071067811865463515, 0.000000000000000000 ) ) ;
#2659=FACE_OUTER_BOUND ( 'NONE', #107936, .T. ) ;
#2661=DIRECTION ( 'NONE',  ( -0.6830127018922181881, 0.6830127018922202975, -0.2588190451025214056 ) ) ;
#2662=ORIENTED_EDGE ( 'NONE', *, *, #20725, .F. ) ;
#2663=DIRECTION ( 'NONE',  ( -0.7071067811865486830, -0.7071067811865464625, 0.000000000000000000 ) ) ;
#2665=ORIENTED_EDGE ( 'NONE', *, *, #125044, .F. ) ;
#2666=LINE ( 'NONE', #132531, #89269 ) ;
#2668=DIRECTION ( 'NONE',  ( -0.000000000000000000, -0.3543493200069152693, 0.9351131265310292928 ) ) ;
#2669=CARTESIAN_POINT ( 'NONE',  ( 19.40370036533107978, 9.134293891043357760, 4.529189151624862575 ) ) ;
#2671=PLANE ( 'NONE',  #39985 ) ;
#2672=CARTESIAN_POINT ( 'NONE',  ( -20.22995720542193254, 21.73644205237998506, 5.000000000000000888 ) ) ;
#2673=EDGE_CURVE ( 'NONE', #36919, #28815, #19379, .T. ) ;
#2674=DIRECTION ( 'NONE',  ( -0.7071067811865487940, 0.7071067811865463515, 0.000000000000000000 ) ) ;
#2676=VECTOR ( 'NONE', #9465, 1000.000000000000000 ) ;
#2678=DIRECTION ( 'NONE',  ( 0.7071067811865487940, 0.7071067811865463515, 0.000000000000000000 ) ) ;
#2679=VECTOR ( 'NONE', #24777, 1000.000000000000227 ) ;
#2680=CARTESIAN_POINT ( 'NONE',  ( -29.29298673570674794, -21.74070752338405299, 4.999753212805210012 ) ) ;
#2681=ORIENTED_EDGE ( 'NONE', *, *, #68927, .T. ) ;
#2682=CARTESIAN_POINT ( 'NONE',  ( -21.29974487139158512, -27.71228299555221142, 4.000000000000000000 ) ) ;
#2683=ORIENTED_EDGE ( 'NONE', *, *, #129377, .F. ) ;
#2685=VECTOR ( 'NONE', #69507, 999.9999999999998863 ) ;
#2686=EDGE_CURVE ( 'NONE', #22961, #80080, #128162, .T. ) ;
#2687=DIRECTION ( 'NONE',  ( -0.7071067811865486830, -0.7071067811865464625, -0.000000000000000000 ) ) ;
#2688=CARTESIAN_POINT ( 'NONE',  ( 19.02964696762728636, -22.22500000000000142, 25.44543266665133885 ) ) ;
#2689=DIRECTION ( 'NONE',  ( -0.7071067811865486830, 0.7071067811865464625, 0.000000000000000000 ) ) ;
#2690=VECTOR ( 'NONE', #78443, 999.9999999999998863 ) ;
#2692=ORIENTED_EDGE ( 'NONE', *, *, #103610, .T. ) ;
#2694=ADVANCED_FACE ( 'NONE', ( #61499 ), #128846, .F. ) ;
#2695=FACE_OUTER_BOUND ( 'NONE', #133482, .T. ) ;
#2696=ORIENTED_EDGE ( 'NONE', *, *, #27152, .T. ) ;
#2697=CARTESIAN_POINT ( 'NONE',  ( -21.48921356237309155, -27.52281430457070499, 5.000000000000000000 ) ) ;
#2698=ADVANCED_FACE ( 'NONE', ( #29522 ), #94775, .F. ) ;
#2699=EDGE_CURVE ( 'NONE', #121977, #75295, #129555, .T. ) ;
#2700=DIRECTION ( 'NONE',  ( -0.7071067811865486830, -0.7071067811865464625, 0.000000000000000000 ) ) ;
#2701=CARTESIAN_POINT ( 'NONE',  ( 23.99451991528749062, 28.92564299267954908, 4.000000000000000000 ) ) ;
#2702=ORIENTED_EDGE ( 'NONE', *, *, #17294, .T. ) ;
#2703=CARTESIAN_POINT ( 'NONE',  ( 5.999999999999970690, 20.96639925780204905, 5.000000000000000000 ) ) ;
#2705=VECTOR ( 'NONE', #46814, 999.9999999999998863 ) ;
#2706=DIRECTION ( 'NONE',  ( -0.000000000000000000, 0.000000000000000000, 1.000000000000000000 ) ) ;
#2707=FACE_OUTER_BOUND ( 'NONE', #18162, .T. ) ;
#2708=FACE_OUTER_BOUND ( 'NONE', #125792, .T. ) ;
#2709=EDGE_CURVE ( 'NONE', #42434, #39115, #139763, .T. ) ;
#2710=EDGE_CURVE ( 'NONE', #89978, #101438, #87498, .T. ) ;
#2711=VERTEX_POINT ( 'NONE', #9166 ) ;
#2713=VERTEX_POINT ( 'NONE', #32411 ) ;
#2715=EDGE_LOOP ( 'NONE', ( #11447, #78910, #72154, #63725 ) ) ;
#2716=EDGE_CURVE ( 'NONE', #26708, #80820, #130306, .T. ) ;
#2717=DIRECTION ( 'NONE',  ( -0.7071067811865486830, -0.7071067811865464625, 0.000000000000000000 ) ) ;
#2718=CARTESIAN_POINT ( 'NONE',  ( -23.99999999999983658, 2.342191155542430181, -5.001666872980029765 ) ) ;
#2720=CARTESIAN_POINT ( 'NONE',  ( 1.499999999999987566, 22.22500000000000142, 4.362957392718795901 ) ) ;
#2721=EDGE_LOOP ( 'NONE', ( #3345, #136037, #40475 ) ) ;
#2722=VECTOR ( 'NONE', #94099, 999.9999999999998863 ) ;
#2724=LINE ( 'NONE', #4823, #130093 ) ;
#2725=CARTESIAN_POINT ( 'NONE',  ( -78.29974487139158157, -27.71228299555260577, 4.000000000000000000 ) ) ;
#2728=CARTESIAN_POINT ( 'NONE',  ( 33.32816939922329880, 20.25929247661551003, 4.000000000000000000 ) ) ;
#2729=AXIS2_PLACEMENT_3D ( 'NONE', #76239, #142911, #128482 ) ;
#2732=CARTESIAN_POINT ( 'NONE',  ( 24.52400138585431577, 22.03583458319438293, 4.979811245910089390 ) ) ;
#2733=AXIS2_PLACEMENT_3D ( 'NONE', #15507, #102583, #123634 ) ;
#2734=DIRECTION ( 'NONE',  ( -0.7071067811865486830, -0.7071067811865464625, 0.000000000000000000 ) ) ;
#2735=EDGE_CURVE ( 'NONE', #128291, #39409, #98380, .T. ) ;
#2736=ORIENTED_EDGE ( 'NONE', *, *, #17084, .F. ) ;
#2738=PLANE ( 'NONE',  #130244 ) ;
#2741=LINE ( 'NONE', #81048, #99795 ) ;
#2742=EDGE_CURVE ( 'NONE', #110817, #65645, #131012, .T. ) ;
#2743=CARTESIAN_POINT ( 'NONE',  ( -5.700255128608413102, -27.71228299555201957, 4.000000000000000000 ) ) ;
#2744=DIRECTION ( 'NONE',  ( 0.7071067811865486830, -0.7071067811865464625, -0.000000000000000000 ) ) ;
#2745=DIRECTION ( 'NONE',  ( -0.7071067811865486830, -0.7071067811865464625, 0.000000000000000000 ) ) ;
#2746=VERTEX_POINT ( 'NONE', #54192 ) ;
#2747=ORIENTED_EDGE ( 'NONE', *, *, #44337, .T. ) ;
#2748=DIRECTION ( 'NONE',  ( 0.3543493200069162685, -0.000000000000000000, -0.9351131265310288487 ) ) ;
#2749=VERTEX_POINT ( 'NONE', #97646 ) ;
#2751=EDGE_CURVE ( 'NONE', #125118, #3555, #86071, .T. ) ;
#2752=VECTOR ( 'NONE', #25053, 1000.000000000000000 ) ;
#2754=VECTOR ( 'NONE', #63417, 1000.000000000000000 ) ;
#2755=DIRECTION ( 'NONE',  ( -0.6830127018922181881, 0.6830127018922202975, -0.2588190451025214056 ) ) ;
#2757=CARTESIAN_POINT ( 'NONE',  ( 18.18398860626898994, 28.73617430169800002, 5.000000000000000000 ) ) ;
#2758=DIRECTION ( 'NONE',  ( -0.7071067811865486830, -0.7071067811865464625, 0.000000000000000000 ) ) ;
#2759=EDGE_CURVE ( 'NONE', #9115, #102939, #20071, .T. ) ;
#2760=VECTOR ( 'NONE', #89125, 1000.000000000000227 ) ;
#2761=LINE ( 'NONE', #13621, #66489 ) ;
#2762=DIRECTION ( 'NONE',  ( 0.6830127018922180770, -0.6830127018922204085, -0.2588190451025213501 ) ) ;
#2763=VECTOR ( 'NONE', #80647, 1000.000000000000000 ) ;
#2764=PLANE ( 'NONE',  #102347 ) ;
#2765=VERTEX_POINT ( 'NONE', #20885 ) ;
#2766=ADVANCED_FACE ( 'NONE', ( #76000 ), #76741, .T. ) ;
#2768=VERTEX_POINT ( 'NONE', #120923 ) ;
#2769=FACE_OUTER_BOUND ( 'NONE', #114331, .T. ) ;
#2771=DIRECTION ( 'NONE',  ( 0.3543493200069162685, -0.000000000000000000, -0.9351131265310288487 ) ) ;
#2772=VERTEX_POINT ( 'NONE', #41953 ) ;
#2773=CARTESIAN_POINT ( 'NONE',  ( -12.48921356237309155, -27.52281430457064104, 5.000000000000000000 ) ) ;
#2774=ORIENTED_EDGE ( 'NONE', *, *, #41427, .T. ) ;
#2775=VERTEX_POINT ( 'NONE', #74591 ) ;
#2779=LINE ( 'NONE', #24538, #995 ) ;
#2781=FACE_OUTER_BOUND ( 'NONE', #60982, .T. ) ;
#2782=EDGE_CURVE ( 'NONE', #18419, #6978, #87589, .T. ) ;
#2784=VECTOR ( 'NONE', #73875, 1000.000000000000000 ) ;
#2787=ADVANCED_FACE ( 'NONE', ( #51407 ), #139856, .T. ) ;
#2788=LINE ( 'NONE', #102842, #97873 ) ;
#2789=FACE_OUTER_BOUND ( 'NONE', #119368, .T. ) ;
#2790=ORIENTED_EDGE ( 'NONE', *, *, #91009, .T. ) ;
#2791=FACE_OUTER_BOUND ( 'NONE', #134953, .T. ) ;
#2792=DIRECTION ( 'NONE',  ( -0.7071067811865486830, -0.7071067811865464625, 0.000000000000000000 ) ) ;
#2793=ORIENTED_EDGE ( 'NONE', *, *, #85, .F. ) ;
#2794=ORIENTED_EDGE ( 'NONE', *, *, #45649, .F. ) ;
#2795=VECTOR ( 'NONE', #136920, 1000.000000000000000 ) ;
#2796=DIRECTION ( 'NONE',  ( -0.7071067811865486830, 0.7071067811865464625, 0.000000000000000000 ) ) ;
#2797=ORIENTED_EDGE ( 'NONE', *, *, #44201, .T. ) ;
#2798=PLANE ( 'NONE',  #5109 ) ;
#2800=CARTESIAN_POINT ( 'NONE',  ( -23.99999999999982592, -19.44781430457063465, 5.000000000000000000 ) ) ;
#2801=LINE ( 'NONE', #135491, #95034 ) ;
#2802=EDGE_CURVE ( 'NONE', #127404, #44686, #54284, .T. ) ;
#2804=CARTESIAN_POINT ( 'NONE',  ( 18.48921356237309510, -27.52281430457068367, 5.000000000000000000 ) ) ;
#2805=AXIS2_PLACEMENT_3D ( 'NONE', #43712, #131445, #88664 ) ;
#2807=CARTESIAN_POINT ( 'NONE',  ( -20.99451991528748707, 28.92564299267952777, 4.000000000000000000 ) ) ;
#2809=VERTEX_POINT ( 'NONE', #40531 ) ;
#2810=PLANE ( 'NONE',  #73735 ) ;
#2811=DIRECTION ( 'NONE',  ( -0.000000000000000000, 0.000000000000000000, 1.000000000000000000 ) ) ;
#2812=ORIENTED_EDGE ( 'NONE', *, *, #34720, .F. ) ;
#2813=EDGE_LOOP ( 'NONE', ( #97197, #71112, #82582, #1452 ) ) ;
#2814=ORIENTED_EDGE ( 'NONE', *, *, #736, .F. ) ;
#2815=DIRECTION ( 'NONE',  ( 0.7071067811865487940, 0.7071067811865463515, 0.000000000000000000 ) ) ;
#2816=DIRECTION ( 'NONE',  ( -0.6830127018922180770, -0.6830127018922204085, -0.2588190451025213501 ) ) ;
#2818=VECTOR ( 'NONE', #46373, 1000.000000000000000 ) ;
#2819=CARTESIAN_POINT ( 'NONE',  ( 18.18268087362628194, -22.22500000000000142, 25.12448555237915926 ) ) ;
#2820=AXIS2_PLACEMENT_3D ( 'NONE', #39865, #84086, #60177 ) ;
#2821=EDGE_LOOP ( 'NONE', ( #114591, #67792, #81456, #68040 ) ) ;
#2822=CARTESIAN_POINT ( 'NONE',  ( 30.18398860626900060, 28.73617430169808173, 5.000000000000000000 ) ) ;
#2824=CARTESIAN_POINT ( 'NONE',  ( 32.20710678118632586, 6.759292476615653023, 5.000000000000000000 ) ) ;
#2825=AXIS2_PLACEMENT_3D ( 'NONE', #33316, #33994, #45608 ) ;
#2826=EDGE_CURVE ( 'NONE', #124530, #3810, #118032, .T. ) ;
#2827=CARTESIAN_POINT ( 'NONE',  ( 5.999999999999960032, 8.966399257802164513, 5.000000000000000000 ) ) ;
#2828=FACE_OUTER_BOUND ( 'NONE', #81836, .T. ) ;
#2829=ORIENTED_EDGE ( 'NONE', *, *, #112687, .T. ) ;
#2830=AXIS2_PLACEMENT_3D ( 'NONE', #71216, #40028, #4429 ) ;
#2833=PLANE ( 'NONE',  #35466 ) ;
#2834=ORIENTED_EDGE ( 'NONE', *, *, #102929, .F. ) ;
#2836=VERTEX_POINT ( 'NONE', #130394 ) ;
#2838=EDGE_CURVE ( 'NONE', #108536, #77576, #96281, .T. ) ;
#2839=CARTESIAN_POINT ( 'NONE',  ( 32.67183060077624646, -15.74070752338412049, 4.000000000000000000 ) ) ;
#2844=LINE ( 'NONE', #13701, #63738 ) ;
#2845=DIRECTION ( 'NONE',  ( 0.7071067811865487940, 0.7071067811865463515, 0.000000000000000000 ) ) ;
#2846=PLANE ( 'NONE',  #127235 ) ;
#2847=CARTESIAN_POINT ( 'NONE',  ( -32.99999999999976552, -6.108550654416993630, -3.114665004255040781 ) ) ;
#2848=CARTESIAN_POINT ( 'NONE',  ( -10.49999999999992539, -9.462702396501018853, -9.474982329943488324 ) ) ;
#2849=LINE ( 'NONE', #100752, #30657 ) ;
#2851=DIRECTION ( 'NONE',  ( -0.7071067811865486830, -0.7071067811865464625, 0.000000000000000000 ) ) ;
#2854=LINE ( 'NONE', #69587, #48219 ) ;
#2855=CARTESIAN_POINT ( 'NONE',  ( 14.20666063542142687, 21.75929247661549937, 4.998822639870700080 ) ) ;
#2856=PLANE ( 'NONE',  #110182 ) ;
#2860=VERTEX_POINT ( 'NONE', #119469 ) ;
#2861=VERTEX_POINT ( 'NONE', #31084 ) ;
#2863=VECTOR ( 'NONE', #65070, 1000.000000000000000 ) ;
#2864=ORIENTED_EDGE ( 'NONE', *, *, #129952, .F. ) ;
#2865=ADVANCED_FACE ( 'NONE', ( #10020 ), #29616, .T. ) ;
#2866=CARTESIAN_POINT ( 'NONE',  ( -32.99999999999977263, 4.384688058510537445, -7.090945410444762231 ) ) ;
#2867=CARTESIAN_POINT ( 'NONE',  ( -29.99999999999978328, -12.41253812416062985, 4.000000000000000000 ) ) ;
#2871=LINE ( 'NONE', #125389, #48633 ) ;
#2872=DIRECTION ( 'NONE',  ( -0.7071067811865487940, 0.7071067811865463515, 0.000000000000000000 ) ) ;
#2873=CARTESIAN_POINT ( 'NONE',  ( 0.000000000000000000, 0.000000000000000000, 5.000000000000000000 ) ) ;
#2875=EDGE_CURVE ( 'NONE', #141302, #134952, #43378, .T. ) ;
#2877=PLANE ( 'NONE',  #129740 ) ;
#2878=CARTESIAN_POINT ( 'NONE',  ( 34.42499999999998295, 10.54139925780192932, 5.000000000000000000 ) ) ;
#2880=CARTESIAN_POINT ( 'NONE',  ( 39.29974487139159578, -27.71228299555233576, 4.000000000000000000 ) ) ;
#2881=CARTESIAN_POINT ( 'NONE',  ( 15.29974487139158867, -27.71228299555216879, 4.000000000000000000 ) ) ;
#2882=CARTESIAN_POINT ( 'NONE',  ( 15.71757738642556568, -21.73023691814493219, 5.000000000000000000 ) ) ;
#2883=CARTESIAN_POINT ( 'NONE',  ( 7.362461875838964609, 22.22500000000000142, 4.000000000000000000 ) ) ;
#2884=EDGE_CURVE ( 'NONE', #90006, #117097, #141240, .T. ) ;
#2885=EDGE_CURVE ( 'NONE', #20632, #105661, #141994, .T. ) ;
#2886=EDGE_LOOP ( 'NONE', ( #3608, #78834, #90700, #136857 ) ) ;
#2887=EDGE_LOOP ( 'NONE', ( #80635, #96807, #108926, #14800 ) ) ;
#2890=EDGE_LOOP ( 'NONE', ( #38959, #26343, #102466, #10380 ) ) ;
#2892=AXIS2_PLACEMENT_3D ( 'NONE', #8924, #19852, #75686 ) ;
#2893=DIRECTION ( 'NONE',  ( -2.781805975412905890E-17, 0.3543493200069152693, 0.9351131265310292928 ) ) ;
#2894=ADVANCED_FACE ( 'NONE', ( #55693 ), #66561, .F. ) ;
#2895=CARTESIAN_POINT ( 'NONE',  ( -2.994519915287485734, 28.92564299267940342, 4.000000000000000000 ) ) ;
#2896=CARTESIAN_POINT ( 'NONE',  ( 6.046588136295404148, 14.25929247661557042, 18.84478104361326345 ) ) ;
#2897=CARTESIAN_POINT ( 'NONE',  ( -12.18398860626900060, 28.73617430169795739, 5.000000000000000000 ) ) ;
#2898=ADVANCED_FACE ( 'NONE', ( #99890 ), #70689, .F. ) ;
#2900=ORIENTED_EDGE ( 'NONE', *, *, #6554, .T. ) ;
#2901=ORIENTED_EDGE ( 'NONE', *, *, #13968, .F. ) ;
#2902=LINE ( 'NONE', #3594, #63916 ) ;
#2904=EDGE_CURVE ( 'NONE', #98425, #96060, #77461, .T. ) ;
#2905=ORIENTED_EDGE ( 'NONE', *, *, #11671, .F. ) ;
#2906=VERTEX_POINT ( 'NONE', #71377 ) ;
#2908=PLANE ( 'NONE',  #12026 ) ;
#2910=VECTOR ( 'NONE', #24639, 1000.000000000000000 ) ;
#2911=EDGE_CURVE ( 'NONE', #6460, #22107, #114837, .T. ) ;
#2913=ORIENTED_EDGE ( 'NONE', *, *, #75065, .T. ) ;
#2914=ORIENTED_EDGE ( 'NONE', *, *, #100813, .F. ) ;
#2915=DIRECTION ( 'NONE',  ( 0.3543493200069162685, -0.000000000000000000, -0.9351131265310288487 ) ) ;
#2916=ORIENTED_EDGE ( 'NONE', *, *, #44396, .T. ) ;
#2917=EDGE_LOOP ( 'NONE', ( #136745, #86290, #53238, #52829 ) ) ;
#2918=VECTOR ( 'NONE', #102357, 1000.000000000000000 ) ;
#2920=AXIS2_PLACEMENT_3D ( 'NONE', #66953, #42365, #100299 ) ;
#2921=VECTOR ( 'NONE', #68999, 1000.000000000000000 ) ;
#2923=AXIS2_PLACEMENT_3D ( 'NONE', #51660, #9534, #110280 ) ;
#2924=EDGE_CURVE ( 'NONE', #50248, #142882, #143391, .T. ) ;
#2925=DIRECTION ( 'NONE',  ( 2.781805975412905890E-17, -0.3543493200069152693, 0.9351131265310292928 ) ) ;
#2926=DIRECTION ( 'NONE',  ( -0.7071067811865487940, 0.7071067811865463515, -0.000000000000000000 ) ) ;
#2927=VERTEX_POINT ( 'NONE', #103266 ) ;
#2928=CARTESIAN_POINT ( 'NONE',  ( -26.99999999999980815, -12.03360074219761700, 5.000000000000000000 ) ) ;
#2930=AXIS2_PLACEMENT_3D ( 'NONE', #104612, #49559, #93741 ) ;
#2932=LINE ( 'NONE', #93523, #27469 ) ;
#2934=FACE_OUTER_BOUND ( 'NONE', #131274, .T. ) ;
#2935=FACE_BOUND ( 'NONE', #8113, .T. ) ;
#2936=ORIENTED_EDGE ( 'NONE', *, *, #19255, .F. ) ;
#2937=LINE ( 'NONE', #47231, #41126 ) ;
#2938=CARTESIAN_POINT ( 'NONE',  ( -13.21498419724181517, -3.740707523384244837, 15.76143240460121220 ) ) ;
#2939=DIRECTION ( 'NONE',  ( 0.7071067811865487940, 0.7071067811865463515, 0.000000000000000000 ) ) ;
#2940=ORIENTED_EDGE ( 'NONE', *, *, #46505, .T. ) ;
#2941=DIRECTION ( 'NONE',  ( 0.7071067811865486830, -0.7071067811865464625, -0.000000000000000000 ) ) ;
#2942=ORIENTED_EDGE ( 'NONE', *, *, #124276, .T. ) ;
#2943=VERTEX_POINT ( 'NONE', #111475 ) ;
#2944=ORIENTED_EDGE ( 'NONE', *, *, #92942, .F. ) ;
#2946=VERTEX_POINT ( 'NONE', #56443 ) ;
#2947=VECTOR ( 'NONE', #92331, 1000.000000000000000 ) ;
#2948=CARTESIAN_POINT ( 'NONE',  ( -33.29974487139158867, -27.71228299555229313, 4.000000000000000000 ) ) ;
#2949=LINE ( 'NONE', #113860, #3317 ) ;
#2950=EDGE_CURVE ( 'NONE', #94849, #25409, #23005, .T. ) ;
#2951=EDGE_LOOP ( 'NONE', ( #106972, #86066, #39161, #121826 ) ) ;
#2952=CARTESIAN_POINT ( 'NONE',  ( 30.32816939922331656, 2.259292476615694323, 4.000000000000000000 ) ) ;
#2953=VECTOR ( 'NONE', #9343, 1000.000000000000000 ) ;
#2954=DIRECTION ( 'NONE',  ( 0.6830127018922181881, 0.6830127018922202975, -0.2588190451025214056 ) ) ;
#2956=CARTESIAN_POINT ( 'NONE',  ( -14.60438740478481989, -0.8081507193758268315, 4.000000000000000000 ) ) ;
#2958=AXIS2_PLACEMENT_3D ( 'NONE', #137286, #26379, #90187 ) ;
#2959=DIRECTION ( 'NONE',  ( 0.7071067811865486830, -0.7071067811865464625, -0.000000000000000000 ) ) ;
#2960=ORIENTED_EDGE ( 'NONE', *, *, #2258, .F. ) ;
#2961=ORIENTED_EDGE ( 'NONE', *, *, #74069, .T. ) ;
#2963=ORIENTED_EDGE ( 'NONE', *, *, #13092, .T. ) ;
#2965=CARTESIAN_POINT ( 'NONE',  ( -2.999999999999981792, -5.527737879153195699, -7.983877177622365373 ) ) ;
#2966=ORIENTED_EDGE ( 'NONE', *, *, #113345, .F. ) ;
#2967=ORIENTED_EDGE ( 'NONE', *, *, #16620, .F. ) ;
#2968=DIRECTION ( 'NONE',  ( 0.3543493200069163240, 0.000000000000000000, -0.9351131265310288487 ) ) ;
#2969=EDGE_CURVE ( 'NONE', #86443, #123774, #30739, .T. ) ;
#2970=CARTESIAN_POINT ( 'NONE',  ( 2.999999999999981792, 7.588810512006216591, -3.013526669885234099 ) ) ;
#2971=ADVANCED_FACE ( 'NONE', ( #138056 ), #85092, .F. ) ;
#2972=ORIENTED_EDGE ( 'NONE', *, *, #112737, .T. ) ;
#2973=DIRECTION ( 'NONE',  ( 0.6830127018922181881, 0.6830127018922202975, -0.2588190451025214056 ) ) ;
#2974=VERTEX_POINT ( 'NONE', #40886 ) ;
#2975=CARTESIAN_POINT ( 'NONE',  ( 23.67183060077630330, -15.74070752338411339, 4.000000000000000000 ) ) ;
#2976=AXIS2_PLACEMENT_3D ( 'NONE', #93608, #126917, #50109 ) ;
#2980=ORIENTED_EDGE ( 'NONE', *, *, #81699, .F. ) ;
#2982=DIRECTION ( 'NONE',  ( 1.000000000000000000, 0.000000000000000000, 0.000000000000000000 ) ) ;
#2983=DIRECTION ( 'NONE',  ( 0.7071067811865486830, -0.7071067811865464625, -0.000000000000000000 ) ) ;
#2984=AXIS2_PLACEMENT_3D ( 'NONE', #16080, #37905, #93694 ) ;
#2985=ORIENTED_EDGE ( 'NONE', *, *, #121994, .F. ) ;
#2986=( NAMED_UNIT ( * ) PLANE_ANGLE_UNIT ( ) SI_UNIT ( $, .RADIAN. ) );
#2987=CARTESIAN_POINT ( 'NONE',  ( 29.99999999999979750, -18.41253812416056235, 4.000000000000000000 ) ) ;
#2988=ORIENTED_EDGE ( 'NONE', *, *, #21911, .T. ) ;
#2989=LINE ( 'NONE', #25450, #117983 ) ;
#2990=VECTOR ( 'NONE', #1431, 1000.000000000000000 ) ;
#2991=DIRECTION ( 'NONE',  ( -0.7071067811865487940, 0.7071067811865463515, 0.000000000000000000 ) ) ;
#2992=LINE ( 'NONE', #91457, #8039 ) ;
#2993=CARTESIAN_POINT ( 'NONE',  ( 15.79289321881335439, -5.240707523384221744, 5.000000000000000000 ) ) ;
#2994=LINE ( 'NONE', #135674, #77317 ) ;
#2995=( BOUNDED_CURVE ( )  B_SPLINE_CURVE ( 3, ( #45291, #122811, #13312, #46743 ),
 .UNSPECIFIED., .F., .F. ) 
 B_SPLINE_CURVE_WITH_KNOTS ( ( 4, 4 ),
 ( 5.043186909253415173, 5.074607125596370949 ),
 .UNSPECIFIED. ) 
 CURVE ( )  GEOMETRIC_REPRESENTATION_ITEM ( )  RATIONAL_B_SPLINE_CURVE ( ( 1.000000000000000000, 0.9999177325257868620, 0.9999177325257868620, 1.000000000000000000 ) ) 
 REPRESENTATION_ITEM ( '' )  );
#2996=ORIENTED_EDGE ( 'NONE', *, *, #16515, .T. ) ;
#2997=EDGE_CURVE ( 'NONE', #139608, #43233, #7516, .T. ) ;
#2998=CARTESIAN_POINT ( 'NONE',  ( 0.000000000000000000, 0.000000000000000000, 5.000000000000000000 ) ) ;
#2999=EDGE_CURVE ( 'NONE', #38388, #85885, #19125, .T. ) ;
#3001=FACE_OUTER_BOUND ( 'NONE', #125880, .T. ) ;
#3002=ORIENTED_EDGE ( 'NONE', *, *, #39321, .T. ) ;
#3004=VECTOR ( 'NONE', #133806, 1000.000000000000000 ) ;
#3005=( BOUNDED_CURVE ( )  B_SPLINE_CURVE ( 3, ( #103964, #48192, #122896, #4608 ),
 .UNSPECIFIED., .F., .F. ) 
 B_SPLINE_CURVE_WITH_KNOTS ( ( 4, 4 ),
 ( 1.901594255663603183, 1.933014472006550966 ),
 .UNSPECIFIED. ) 
 CURVE ( )  GEOMETRIC_REPRESENTATION_ITEM ( )  RATIONAL_B_SPLINE_CURVE ( ( 1.000000000000000000, 0.9999177325257868620, 0.9999177325257868620, 1.000000000000000000 ) ) 
 REPRESENTATION_ITEM ( '' )  );
#3006=LINE ( 'NONE', #47979, #74788 ) ;
#3007=ORIENTED_EDGE ( 'NONE', *, *, #14711, .T. ) ;
#3008=DIRECTION ( 'NONE',  ( -0.7071067811865487940, 0.7071067811865463515, 0.000000000000000000 ) ) ;
#3009=VERTEX_POINT ( 'NONE', #40203 ) ;
#3012=VECTOR ( 'NONE', #15009, 1000.000000000000000 ) ;
#3013=DIRECTION ( 'NONE',  ( -0.7071067811865486830, -0.7071067811865464625, 0.000000000000000000 ) ) ;
#3014=CARTESIAN_POINT ( 'NONE',  ( -20.99999999999985789, -10.77435723561697145, -9.972017380717186796 ) ) ;
#3015=VERTEX_POINT ( 'NONE', #29987 ) ;
#3017=DIRECTION ( 'NONE',  ( 0.6830127018922180770, -0.6830127018922204085, -0.2588190451025213501 ) ) ;
#3018=ORIENTED_EDGE ( 'NONE', *, *, #80098, .F. ) ;
#3020=CARTESIAN_POINT ( 'NONE',  ( -15.79289321881334196, -17.24070752338410628, 5.000000000000000000 ) ) ;
#3021=DIRECTION ( 'NONE',  ( 0.3543493200069162685, -0.000000000000000000, -0.9351131265310288487 ) ) ;
#3022=AXIS2_PLACEMENT_3D ( 'NONE', #120297, #10833, #42094 ) ;
#3023=DIRECTION ( 'NONE',  ( -0.7071067811865487940, 0.7071067811865463515, 0.000000000000000000 ) ) ;
#3026=DIRECTION ( 'NONE',  ( -0.000000000000000000, 0.000000000000000000, 1.000000000000000000 ) ) ;
#3027=ORIENTED_EDGE ( 'NONE', *, *, #61422, .T. ) ;
#3028=AXIS2_PLACEMENT_3D ( 'NONE', #48625, #60233, #136331 ) ;
#3029=VERTEX_POINT ( 'NONE', #28593 ) ;
#3032=ORIENTED_EDGE ( 'NONE', *, *, #74849, .F. ) ;
#3033=EDGE_LOOP ( 'NONE', ( #122028, #131656, #46271 ) ) ;
#3034=ORIENTED_EDGE ( 'NONE', *, *, #43142, .T. ) ;
#3035=AXIS2_PLACEMENT_3D ( 'NONE', #94451, #114758, #70619 ) ;
#3036=DIRECTION ( 'NONE',  ( -0.6830127018922181881, 0.6830127018922202975, -0.2588190451025214056 ) ) ;
#3037=ORIENTED_EDGE ( 'NONE', *, *, #70665, .F. ) ;
#3038=DIRECTION ( 'NONE',  ( 0.7071067811865487940, -0.7071067811865463515, 0.000000000000000000 ) ) ;
#3039=DIRECTION ( 'NONE',  ( 0.7071067811865486830, -0.7071067811865464625, -0.000000000000000000 ) ) ;
#3040=PLANE ( 'NONE',  #81060 ) ;
#3041=CARTESIAN_POINT ( 'NONE',  ( -17.99999999999987210, 12.83542986846995504, -1.025386466790330076 ) ) ;
#3043=ORIENTED_EDGE ( 'NONE', *, *, #27290, .F. ) ;
#3044=ADVANCED_FACE ( 'NONE', ( #72850 ), #17672, .T. ) ;
#3045=DIRECTION ( 'NONE',  ( -2.781805975412905890E-17, 0.3543493200069152693, 0.9351131265310292928 ) ) ;
#3046=DIRECTION ( 'NONE',  ( -0.3543493200069162685, -0.000000000000000000, -0.9351131265310288487 ) ) ;
#3048=LINE ( 'NONE', #137878, #142172 ) ;
#3049=DIRECTION ( 'NONE',  ( -0.7071067811865487940, 0.7071067811865463515, -0.000000000000000000 ) ) ;
#3050=CARTESIAN_POINT ( 'NONE',  ( -2.999999999999968026, 11.96639925780214675, 5.000000000000000000 ) ) ;
#3051=LINE ( 'NONE', #25515, #107019 ) ;
#3052=DIRECTION ( 'NONE',  ( -0.000000000000000000, -0.3543493200069152693, 0.9351131265310292928 ) ) ;
#3054=CARTESIAN_POINT ( 'NONE',  ( 2.207106781186528810, 9.759292476615625489, 5.000000000000000000 ) ) ;
#3055=EDGE_CURVE ( 'NONE', #136825, #90110, #115538, .T. ) ;
#3056=VECTOR ( 'NONE', #44435, 1000.000000000000000 ) ;
#3057=CARTESIAN_POINT ( 'NONE',  ( -31.17183060077625356, -5.240707523384225297, 4.000000000000000000 ) ) ;
#3058=EDGE_LOOP ( 'NONE', ( #17079, #6653, #115395, #37668 ) ) ;
#3059=ORIENTED_EDGE ( 'NONE', *, *, #103222, .T. ) ;
#3061=ADVANCED_FACE ( 'NONE', ( #61945 ), #106095, .F. ) ;
#3062=VERTEX_POINT ( 'NONE', #85801 ) ;
#3063=VERTEX_POINT ( 'NONE', #51773 ) ;
#3064=DIRECTION ( 'NONE',  ( 0.7071067811865487940, 0.7071067811865463515, 0.000000000000000000 ) ) ;
#3065=ADVANCED_FACE ( 'NONE', ( #128605 ), #116295, .F. ) ;
#3066=CARTESIAN_POINT ( 'NONE',  ( -26.70025512860841488, -27.71228299555187391, 4.000000000000000000 ) ) ;
#3067=ORIENTED_EDGE ( 'NONE', *, *, #120246, .F. ) ;
#3069=CARTESIAN_POINT ( 'NONE',  ( -47.99451991528749062, 28.92564299267971251, 4.000000000000000000 ) ) ;
#3070=VECTOR ( 'NONE', #281, 1000.000000000000000 ) ;
#3071=CARTESIAN_POINT ( 'NONE',  ( -23.27718569542924243, -21.72500000000000142, 5.000000000000000000 ) ) ;
#3073=VECTOR ( 'NONE', #82646, 1000.000000000000000 ) ;
#3074=VERTEX_POINT ( 'NONE', #29279 ) ;
#3076=DIRECTION ( 'NONE',  ( 0.7071067811865486830, -0.7071067811865464625, -0.000000000000000000 ) ) ;
#3079=CARTESIAN_POINT ( 'NONE',  ( -13.49999999999990408, -20.53675388469232033, 2.352720554255862684 ) ) ;
#3080=CARTESIAN_POINT ( 'NONE',  ( 42.18398860626899705, 28.73617430169816700, 5.000000000000000000 ) ) ;
#3081=AXIS2_PLACEMENT_3D ( 'NONE', #58344, #80078, #59053 ) ;
#3082=ADVANCED_FACE ( 'NONE', ( #117682 ), #107552, .F. ) ;
#3083=DIRECTION ( 'NONE',  ( -0.7071067811865486830, -0.7071067811865464625, 0.000000000000000000 ) ) ;
#3084=VERTEX_POINT ( 'NONE', #127160 ) ;
#3085=ADVANCED_FACE ( 'NONE', ( #41580 ), #105406, .F. ) ;
#3086=ORIENTED_EDGE ( 'NONE', *, *, #89982, .F. ) ;
#3087=CARTESIAN_POINT ( 'NONE',  ( -39.48921356237310221, -27.52281430457082934, 5.000000000000000000 ) ) ;
#3088=CARTESIAN_POINT ( 'NONE',  ( 72.18398860626899705, 28.73617430169837661, 5.000000000000000000 ) ) ;
#3089=CARTESIAN_POINT ( 'NONE',  ( 3.792893218813435663, -14.24070752338414003, 5.000000000000000000 ) ) ;
#3090=CARTESIAN_POINT ( 'NONE',  ( 21.70710678118639692, 14.25929247661557042, 5.000000000000000000 ) ) ;
#3091=DIRECTION ( 'NONE',  ( 0.6830127018922181881, 0.6830127018922202975, -0.2588190451025214056 ) ) ;
#3092=EDGE_CURVE ( 'NONE', #11574, #83476, #76372, .T. ) ;
#3093=VECTOR ( 'NONE', #41639, 1000.000000000000114 ) ;
#3094=VECTOR ( 'NONE', #128024, 1000.000000000000000 ) ;
#3096=LINE ( 'NONE', #49509, #132227 ) ;
#3097=DIRECTION ( 'NONE',  ( 0.7071067811865487940, -0.7071067811865463515, -0.000000000000000000 ) ) ;
#3098=ORIENTED_EDGE ( 'NONE', *, *, #41692, .T. ) ;
#3099=ORIENTED_EDGE ( 'NONE', *, *, #84317, .F. ) ;
#3102=EDGE_LOOP ( 'NONE', ( #88999, #8435, #140131, #20316 ) ) ;
#3103=PLANE ( 'NONE',  #60435 ) ;
#3104=ORIENTED_EDGE ( 'NONE', *, *, #100168, .T. ) ;
#3107=AXIS2_PLACEMENT_3D ( 'NONE', #35709, #113207, #26225 ) ;
#3108=DIRECTION ( 'NONE',  ( 0.7071067811865487940, -0.7071067811865463515, 0.000000000000000000 ) ) ;
#3109=FACE_BOUND ( 'NONE', #51793, .T. ) ;
#3110=CARTESIAN_POINT ( 'NONE',  ( 3.707106781186521705, 8.259292476615639700, 5.000000000000000000 ) ) ;
#3111=FACE_OUTER_BOUND ( 'NONE', #14633, .T. ) ;
#3112=DIRECTION ( 'NONE',  ( -0.7071067811865486830, -0.7071067811865464625, -0.000000000000000000 ) ) ;
#3113=VERTEX_POINT ( 'NONE', #43039 ) ;
#3114=CARTESIAN_POINT ( 'NONE',  ( 28.49999999999980460, 11.52377502935405751, -1.522421517564149118 ) ) ;
#3115=ADVANCED_FACE ( 'NONE', ( #21970 ), #10371, .F. ) ;
#3116=ORIENTED_EDGE ( 'NONE', *, *, #117463, .F. ) ;
#3119=VECTOR ( 'NONE', #99052, 999.9999999999998863 ) ;
#3120=EDGE_LOOP ( 'NONE', ( #42000, #40558, #71469, #78975 ) ) ;
#3121=CARTESIAN_POINT ( 'NONE',  ( -11.67183060077638679, 17.25929247661554200, 4.000000000000000000 ) ) ;
#3122=EDGE_CURVE ( 'NONE', #72171, #12168, #11067, .T. ) ;
#3123=ORIENTED_EDGE ( 'NONE', *, *, #75155, .T. ) ;
#3125=VECTOR ( 'NONE', #100669, 1000.000000000000000 ) ;
#3126=CARTESIAN_POINT ( 'NONE',  ( 17.99999999999987566, -8.151047557385048492, -8.977947279169839589 ) ) ;
#3127=DIRECTION ( 'NONE',  ( -0.7071067811865487940, 0.7071067811865463515, -0.000000000000000000 ) ) ;
#3128=ADVANCED_FACE ( 'NONE', ( #120541 ), #11793, .F. ) ;
#3129=CARTESIAN_POINT ( 'NONE',  ( -22.94330788408294808, -22.22500000000000142, 9.540311041892492128 ) ) ;
#3130=DIRECTION ( 'NONE',  ( 1.000000000000000000, 0.000000000000000000, 0.000000000000000000 ) ) ;
#3131=FACE_OUTER_BOUND ( 'NONE', #101997, .T. ) ;
#3132=CARTESIAN_POINT ( 'NONE',  ( 69.18398860626899705, 28.73617430169835529, 5.000000000000000000 ) ) ;
#3133=DIRECTION ( 'NONE',  ( -0.7071067811865487940, 0.7071067811865463515, 0.000000000000000000 ) ) ;
#3134=ORIENTED_EDGE ( 'NONE', *, *, #12577, .T. ) ;
#3135=EDGE_CURVE ( 'NONE', #62769, #84933, #96668, .T. ) ;
#3136=ORIENTED_EDGE ( 'NONE', *, *, #80394, .F. ) ;
#3137=LINE ( 'NONE', #16888, #91358 ) ;
#3138=PLANE ( 'NONE',  #60625 ) ;
#3139=ORIENTED_EDGE ( 'NONE', *, *, #95939, .F. ) ;
#3142=ADVANCED_FACE ( 'NONE', ( #130772 ), #65529, .F. ) ;
#3144=DIRECTION ( 'NONE',  ( 0.7071067811865486830, -0.7071067811865464625, -0.000000000000000000 ) ) ;
#3146=AXIS2_PLACEMENT_3D ( 'NONE', #70913, #83197, #103489 ) ;
#3147=FACE_OUTER_BOUND ( 'NONE', #18353, .T. ) ;
#3148=VECTOR ( 'NONE', #94137, 999.9999999999998863 ) ;
#3151=EDGE_LOOP ( 'NONE', ( #4845, #49636, #132721, #119062 ) ) ;
#3152=DIRECTION ( 'NONE',  ( 1.000000000000000000, 0.000000000000000000, 0.000000000000000000 ) ) ;
#3153=DIRECTION ( 'NONE',  ( -0.7071067811865486830, -0.7071067811865464625, 0.000000000000000000 ) ) ;
#3154=CARTESIAN_POINT ( 'NONE',  ( -21.48921356237309155, -27.52281430457070499, 5.000000000000000000 ) ) ;
#3155=DIRECTION ( 'NONE',  ( 0.7071067811865487940, -0.7071067811865463515, 0.000000000000000000 ) ) ;
#3156=ORIENTED_EDGE ( 'NONE', *, *, #1709, .T. ) ;
#3157=VERTEX_POINT ( 'NONE', #53163 ) ;
#3158=DIRECTION ( 'NONE',  ( 0.7071067811865486830, -0.7071067811865464625, -0.000000000000000000 ) ) ;
#3159=DIRECTION ( 'NONE',  ( 1.000000000000000000, 0.000000000000000000, 0.000000000000000000 ) ) ;
#3161=DIRECTION ( 'NONE',  ( 1.000000000000000000, 0.000000000000000000, 0.000000000000000000 ) ) ;
#3162=ORIENTED_EDGE ( 'NONE', *, *, #15930, .F. ) ;
#3163=CARTESIAN_POINT ( 'NONE',  ( 20.87852683662840292, -20.24070752338407075, 7.412974875817742948 ) ) ;
#3164=DIRECTION ( 'NONE',  ( 0.7071067811865486830, -0.7071067811865464625, -0.000000000000000000 ) ) ;
#3165=EDGE_CURVE ( 'NONE', #134283, #95889, #109703, .T. ) ;
#3166=AXIS2_PLACEMENT_3D ( 'NONE', #120457, #31364, #65444 ) ;
#3167=CARTESIAN_POINT ( 'NONE',  ( -29.99999999999979039, -6.412538124160687580, 4.000000000000000000 ) ) ;
#3168=CARTESIAN_POINT ( 'NONE',  ( 48.48921356237309510, -27.52281430457089328, 5.000000000000000000 ) ) ;
#3169=ORIENTED_EDGE ( 'NONE', *, *, #56125, .F. ) ;
#3171=CARTESIAN_POINT ( 'NONE',  ( -23.48334561358938899, 22.22500000000000142, 4.500000000000000888 ) ) ;
#3173=VECTOR ( 'NONE', #18312, 1000.000000000000227 ) ;
#3174=CARTESIAN_POINT ( 'NONE',  ( -5.994519915287488843, 28.92564299267942118, 4.000000000000000000 ) ) ;
#3175=ADVANCED_FACE ( 'NONE', ( #66218 ), #121986, .F. ) ;
#3176=DIRECTION ( 'NONE',  ( 0.7071067811865487940, 0.7071067811865463515, -0.000000000000000000 ) ) ;
#3178=ADVANCED_FACE ( 'NONE', ( #43730 ), #99514, .F. ) ;
#3179=VERTEX_POINT ( 'NONE', #77112 ) ;
#3183=( BOUNDED_CURVE ( )  B_SPLINE_CURVE ( 3, ( #109716, #43750, #21982, #85814 ),
 .UNSPECIFIED., .F., .T. ) 
 B_SPLINE_CURVE_WITH_KNOTS ( ( 4, 4 ),
 ( 2.779374508378132713, 4.199602562396792749 ),
 .UNSPECIFIED. ) 
 CURVE ( )  GEOMETRIC_REPRESENTATION_ITEM ( )  RATIONAL_B_SPLINE_CURVE ( ( 1.000000000000000000, 0.8388583629366723748, 0.8388583629366723748, 1.000000000000000000 ) ) 
 REPRESENTATION_ITEM ( '' )  );
#3184=AXIS2_PLACEMENT_3D ( 'NONE', #101386, #134032, #2031 ) ;
#3186=LINE ( 'NONE', #91639, #110683 ) ;
#3187=VECTOR ( 'NONE', #115094, 1000.000000000000000 ) ;
#3188=DIRECTION ( 'NONE',  ( -0.000000000000000000, 0.3543493200069153248, 0.9351131265310292928 ) ) ;
#3189=LINE ( 'NONE', #13341, #101572 ) ;
#3191=EDGE_LOOP ( 'NONE', ( #81785, #13339, #15057, #105868 ) ) ;
#3193=CARTESIAN_POINT ( 'NONE',  ( 3.299744871391591339, -27.71228299555208352, 4.000000000000000000 ) ) ;
#3194=VECTOR ( 'NONE', #44596, 1000.000000000000000 ) ;
#3195=DIRECTION ( 'NONE',  ( -0.6830127018922180770, -0.6830127018922204085, -0.2588190451025213501 ) ) ;
#3197=ADVANCED_FACE ( 'NONE', ( #121288 ), #88688, .T. ) ;
#3198=FACE_OUTER_BOUND ( 'NONE', #17576, .T. ) ;
#3199=ORIENTED_EDGE ( 'NONE', *, *, #34344, .T. ) ;
#3200=CARTESIAN_POINT ( 'NONE',  ( -20.99999999999985079, -18.03360074219755660, 5.000000000000000000 ) ) ;
#3204=DIRECTION ( 'NONE',  ( 0.7071067811865487940, -0.7071067811865463515, 0.000000000000000000 ) ) ;
#3205=CARTESIAN_POINT ( 'NONE',  ( -11.20710678118646797, 15.75929247661555976, 5.000000000000000000 ) ) ;
#3207=CARTESIAN_POINT ( 'NONE',  ( -21.18398860626899349, 28.73617430169802134, 5.000000000000000000 ) ) ;
#3208=CARTESIAN_POINT ( 'NONE',  ( -11.99999999999991473, -0.03360074219773377668, 5.000000000000000000 ) ) ;
#3209=EDGE_LOOP ( 'NONE', ( #31867, #53769, #7795, #72141 ) ) ;
#3210=VERTEX_POINT ( 'NONE', #56080 ) ;
#3211=DIRECTION ( 'NONE',  ( -0.7071067811865486830, -0.7071067811865464625, 0.000000000000000000 ) ) ;
#3212=PLANE ( 'NONE',  #58477 ) ;
#3213=CARTESIAN_POINT ( 'NONE',  ( 1.371765549556144048, -8.240707523384196875, 11.38925528200752169 ) ) ;
#3216=PLANE ( 'NONE',  #78724 ) ;
#3218=VECTOR ( 'NONE', #79720, 1000.000000000000000 ) ;
#3219=CARTESIAN_POINT ( 'NONE',  ( 69.48921356237309510, -27.52281430457103895, 5.000000000000000000 ) ) ;
#3220=ORIENTED_EDGE ( 'NONE', *, *, #10733, .T. ) ;
#3224=DIRECTION ( 'NONE',  ( 0.7071067811865487940, 0.7071067811865463515, 0.000000000000000000 ) ) ;
#3225=FACE_OUTER_BOUND ( 'NONE', #76005, .T. ) ;
#3226=ORIENTED_EDGE ( 'NONE', *, *, #79951, .T. ) ;
#3227=EDGE_CURVE ( 'NONE', #53161, #86656, #8895, .T. ) ;
#3228=ADVANCED_FACE ( 'NONE', ( #20523 ), #64782, .F. ) ;
#3229=VECTOR ( 'NONE', #53043, 1000.000000000000000 ) ;
#3230=LINE ( 'NONE', #57660, #83808 ) ;
#3231=DIRECTION ( 'NONE',  ( -0.000000000000000000, 0.000000000000000000, 1.000000000000000000 ) ) ;
#3233=LINE ( 'NONE', #102586, #32160 ) ;
#3235=VERTEX_POINT ( 'NONE', #68382 ) ;
#3236=DIRECTION ( 'NONE',  ( -0.7071067811865486830, 0.7071067811865464625, 0.000000000000000000 ) ) ;
#3237=DIRECTION ( 'NONE',  ( 0.6830127018922180770, -0.6830127018922204085, -0.2588190451025213501 ) ) ;
#3240=EDGE_CURVE ( 'NONE', #23652, #32623, #78510, .T. ) ;
#3243=VERTEX_POINT ( 'NONE', #24834 ) ;
#3244=CARTESIAN_POINT ( 'NONE',  ( 16.49999999999988276, 22.22500000000000142, 4.362957392718795901 ) ) ;
#3246=DIRECTION ( 'NONE',  ( 0.000000000000000000, 0.000000000000000000, -1.000000000000000000 ) ) ;
#3247=VECTOR ( 'NONE', #43984, 1000.000000000000000 ) ;
#3249=VERTEX_POINT ( 'NONE', #13221 ) ;
#3251=VERTEX_POINT ( 'NONE', #124863 ) ;
#3252=VECTOR ( 'NONE', #101289, 1000.000000000000227 ) ;
#3253=EDGE_LOOP ( 'NONE', ( #29575, #123693, #89337 ) ) ;
#3254=LINE ( 'NONE', #114853, #52206 ) ;
#3255=LINE ( 'NONE', #124340, #36458 ) ;
#3258=CARTESIAN_POINT ( 'NONE',  ( 16.49999999999988276, -12.66682484999664737, -0.6294897503863559063 ) ) ;
#3260=ORIENTED_EDGE ( 'NONE', *, *, #43213, .T. ) ;
#3261=EDGE_CURVE ( 'NONE', #110799, #32452, #4435, .T. ) ;
#3262=DIRECTION ( 'NONE',  ( 0.6830127018922180770, -0.6830127018922204085, -0.2588190451025213501 ) ) ;
#3265=AXIS2_PLACEMENT_3D ( 'NONE', #68836, #122454, #44969 ) ;
#3267=DIRECTION ( 'NONE',  ( 0.3543493200069162685, -0.000000000000000000, -0.9351131265310288487 ) ) ;
#3269=CARTESIAN_POINT ( 'NONE',  ( 25.49999999999983658, -5.947814304570765209, 5.000000000000000000 ) ) ;
#3270=ORIENTED_EDGE ( 'NONE', *, *, #30413, .F. ) ;
#3271=VECTOR ( 'NONE', #122625, 1000.000000000000000 ) ;
#3272=FACE_BOUND ( 'NONE', #53399, .T. ) ;
#3273=LINE ( 'NONE', #69280, #13162 ) ;
#3274=DIRECTION ( 'NONE',  ( -0.000000000000000000, 0.000000000000000000, 1.000000000000000000 ) ) ;
#3275=FACE_OUTER_BOUND ( 'NONE', #110605, .T. ) ;
#3277=PLANE ( 'NONE',  #108171 ) ;
#3280=ADVANCED_FACE ( 'NONE', ( #59640 ), #67673, .T. ) ;
#3281=VERTEX_POINT ( 'NONE', #92216 ) ;
#3282=AXIS2_PLACEMENT_3D ( 'NONE', #1008, #45290, #89464 ) ;
#3283=VERTEX_POINT ( 'NONE', #13936 ) ;
#3285=EDGE_LOOP ( 'NONE', ( #15701, #137223, #112251, #40560 ) ) ;
#3286=DIRECTION ( 'NONE',  ( -0.7071067811865486830, 0.7071067811865464625, 0.000000000000000000 ) ) ;
#3287=ORIENTED_EDGE ( 'NONE', *, *, #137131, .F. ) ;
#3288=DIRECTION ( 'NONE',  ( 0.6830127018922180770, -0.6830127018922204085, -0.2588190451025213501 ) ) ;
#3289=CARTESIAN_POINT ( 'NONE',  ( -24.48921356237309510, -27.52281430457072631, 5.000000000000000000 ) ) ;
#3290=FACE_OUTER_BOUND ( 'NONE', #61967, .T. ) ;
#3291=ORIENTED_EDGE ( 'NONE', *, *, #108340, .T. ) ;
#3292=FACE_OUTER_BOUND ( 'NONE', #19326, .T. ) ;
#3293=AXIS2_PLACEMENT_3D ( 'NONE', #63467, #17073, #117074 ) ;
#3295=EDGE_CURVE ( 'NONE', #119191, #73062, #101674, .T. ) ;
#3296=DIRECTION ( 'NONE',  ( 0.3543493200069162685, -0.000000000000000000, -0.9351131265310288487 ) ) ;
#3297=DIRECTION ( 'NONE',  ( -0.7071067811865486830, -0.7071067811865464625, 0.000000000000000000 ) ) ;
#3298=DIRECTION ( 'NONE',  ( -0.000000000000000000, -0.3543493200069152693, 0.9351131265310292928 ) ) ;
#3299=ORIENTED_EDGE ( 'NONE', *, *, #7862, .T. ) ;
#3300=LINE ( 'NONE', #93892, #79047 ) ;
#3301=ORIENTED_EDGE ( 'NONE', *, *, #50801, .F. ) ;
#3302=ORIENTED_EDGE ( 'NONE', *, *, #33053, .T. ) ;
#3303=EDGE_CURVE ( 'NONE', #85379, #44481, #134328, .T. ) ;
#3304=VERTEX_POINT ( 'NONE', #2334 ) ;
#3306=ORIENTED_EDGE ( 'NONE', *, *, #28430, .F. ) ;
#3308=DIRECTION ( 'NONE',  ( -0.7071067811865486830, -0.7071067811865464625, -0.000000000000000000 ) ) ;
#3310=DIRECTION ( 'NONE',  ( 0.7071067811865486830, -0.7071067811865464625, -0.000000000000000000 ) ) ;
#3311=VERTEX_POINT ( 'NONE', #35029 ) ;
#3313=ADVANCED_FACE ( 'NONE', ( #114685 ), #48748, .F. ) ;
#3314=DIRECTION ( 'NONE',  ( -0.6830127018922180770, -0.6830127018922204085, -0.2588190451025213501 ) ) ;
#3315=ORIENTED_EDGE ( 'NONE', *, *, #23637, .F. ) ;
#3317=VECTOR ( 'NONE', #14555, 999.9999999999998863 ) ;
#3318=CARTESIAN_POINT ( 'NONE',  ( -45.18398860626900415, 28.73617430169818832, 5.000000000000000000 ) ) ;
#3319=CARTESIAN_POINT ( 'NONE',  ( -14.99999999999988454, -13.44781430457069149, 5.000000000000000000 ) ) ;
#3321=VERTEX_POINT ( 'NONE', #47369 ) ;
#3322=PLANE ( 'NONE',  #115201 ) ;
#3323=EDGE_CURVE ( 'NONE', #119026, #83338, #100961, .T. ) ;
#3325=ORIENTED_EDGE ( 'NONE', *, *, #89367, .F. ) ;
#3326=VERTEX_POINT ( 'NONE', #112561 ) ;
#3327=CARTESIAN_POINT ( 'NONE',  ( -33.29974487139158867, -27.71228299555229313, 4.000000000000000000 ) ) ;
#3329=PLANE ( 'NONE',  #60984 ) ;
#3330=EDGE_CURVE ( 'NONE', #106116, #36944, #91535, .T. ) ;
#3331=DIRECTION ( 'NONE',  ( -0.7071067811865486830, -0.7071067811865464625, -0.000000000000000000 ) ) ;
#3332=EDGE_CURVE ( 'NONE', #118907, #89121, #69079, .T. ) ;
#3333=CARTESIAN_POINT ( 'NONE',  ( -36.48921356237310221, -27.52281430457080802, 5.000000000000000000 ) ) ;
#3334=VERTEX_POINT ( 'NONE', #46650 ) ;
#3335=VECTOR ( 'NONE', #37942, 999.9999999999998863 ) ;
#3336=CARTESIAN_POINT ( 'NONE',  ( -28.17183060077627133, -11.24070752338416845, 4.000000000000000000 ) ) ;
#3337=AXIS2_PLACEMENT_3D ( 'NONE', #100074, #32687, #98623 ) ;
#3339=CARTESIAN_POINT ( 'NONE',  ( 32.84387692260735747, -22.22499999999999787, 4.000000000000000000 ) ) ;
#3340=DIRECTION ( 'NONE',  ( -0.000000000000000000, -0.3543493200069153248, -0.9351131265310291818 ) ) ;
#3343=ORIENTED_EDGE ( 'NONE', *, *, #80401, .F. ) ;
#3344=AXIS2_PLACEMENT_3D ( 'NONE', #59086, #82942, #15493 ) ;
#3345=ORIENTED_EDGE ( 'NONE', *, *, #65365, .T. ) ;
#3346=ORIENTED_EDGE ( 'NONE', *, *, #120387, .T. ) ;
#3348=CARTESIAN_POINT ( 'NONE',  ( 62.99451991528749772, 28.92564299267982264, 4.000000000000000000 ) ) ;
#3349=DIRECTION ( 'NONE',  ( -0.7071067811865486830, 0.7071067811865464625, 0.000000000000000000 ) ) ;
#3350=FACE_OUTER_BOUND ( 'NONE', #104036, .T. ) ;
#3351=DIRECTION ( 'NONE',  ( 0.3543493200069162685, -0.000000000000000000, -0.9351131265310288487 ) ) ;
#3357=LINE ( 'NONE', #102708, #18824 ) ;
#3358=DIRECTION ( 'NONE',  ( 0.6830127018922180770, -0.6830127018922204085, -0.2588190451025213501 ) ) ;
#3359=ORIENTED_EDGE ( 'NONE', *, *, #79397, .T. ) ;
#3360=ORIENTED_EDGE ( 'NONE', *, *, #73043, .F. ) ;
#3361=DIRECTION ( 'NONE',  ( 0.7071067811865486830, -0.7071067811865464625, -0.000000000000000000 ) ) ;
#3363=ORIENTED_EDGE ( 'NONE', *, *, #120365, .F. ) ;
#3365=PLANE ( 'NONE',  #28683 ) ;
#3366=VERTEX_POINT ( 'NONE', #81398 ) ;
#3367=LINE ( 'NONE', #25860, #53152 ) ;
#3368=ORIENTED_EDGE ( 'NONE', *, *, #62813, .F. ) ;
#3370=EDGE_LOOP ( 'NONE', ( #40981, #44896, #79051, #110407 ) ) ;
#3371=VECTOR ( 'NONE', #46007, 1000.000000000000227 ) ;
#3372=LINE ( 'NONE', #36736, #112148 ) ;
#3374=CARTESIAN_POINT ( 'NONE',  ( -24.18398860626899705, 28.73617430169804265, 5.000000000000000000 ) ) ;
#3375=VECTOR ( 'NONE', #70458, 1000.000000000000000 ) ;
#3376=AXIS2_PLACEMENT_3D ( 'NONE', #23881, #68146, #12973 ) ;
#3377=EDGE_CURVE ( 'NONE', #107847, #20599, #26278, .T. ) ;
#3379=DIRECTION ( 'NONE',  ( -0.7071067811865487940, 0.7071067811865463515, 0.000000000000000000 ) ) ;
#3380=FACE_OUTER_BOUND ( 'NONE', #130926, .T. ) ;
#3381=ADVANCED_FACE ( 'NONE', ( #116120 ), #29819, .F. ) ;
#3382=CARTESIAN_POINT ( 'NONE',  ( 17.81601139373099940, 28.73617430169775133, 5.000000000000000000 ) ) ;
#3388=ADVANCED_FACE ( 'NONE', ( #107389 ), #16822, .F. ) ;
#3389=EDGE_CURVE ( 'NONE', #65237, #14379, #8056, .T. ) ;
#3390=DIRECTION ( 'NONE',  ( -0.6830127018922180770, -0.6830127018922204085, -0.2588190451025213501 ) ) ;
#3391=EDGE_LOOP ( 'NONE', ( #34059, #68348, #105271, #88265 ) ) ;
#3393=DIRECTION ( 'NONE',  ( 0.7071067811865486830, -0.7071067811865464625, -0.000000000000000000 ) ) ;
#3394=CARTESIAN_POINT ( 'NONE',  ( 9.299744871391588674, -27.71228299555212971, 4.000000000000000000 ) ) ;
#3395=DIRECTION ( 'NONE',  ( 0.6830127018922181881, 0.6830127018922202975, -0.2588190451025214056 ) ) ;
#3397=ORIENTED_EDGE ( 'NONE', *, *, #39565, .F. ) ;
#3399=DIRECTION ( 'NONE',  ( -0.7071067811865487940, 0.7071067811865463515, -0.000000000000000000 ) ) ;
#3400=ADVANCED_FACE ( 'NONE', ( #105939 ), #5199, .F. ) ;
#3402=CARTESIAN_POINT ( 'NONE',  ( -24.20969143188526118, 6.176090689687629975, 5.000000000000000000 ) ) ;
#3403=EDGE_CURVE ( 'NONE', #19559, #24434, #106655, .T. ) ;
#3404=DIRECTION ( 'NONE',  ( 0.7071067811865486830, -0.7071067811865464625, -0.000000000000000000 ) ) ;
#3405=LINE ( 'NONE', #104136, #142364 ) ;
#3406=VERTEX_POINT ( 'NONE', #105253 ) ;
#3407=CARTESIAN_POINT ( 'NONE',  ( -4.499999999999976019, 19.08746187583905751, 4.000000000000000000 ) ) ;
#3408=CARTESIAN_POINT ( 'NONE',  ( -77.99451991528749772, 28.92564299267992567, 4.000000000000000000 ) ) ;
#3409=CARTESIAN_POINT ( 'NONE',  ( 24.18398860626899705, 28.73617430169804265, 5.000000000000000000 ) ) ;
#3411=ORIENTED_EDGE ( 'NONE', *, *, #12605, .T. ) ;
#3412=VERTEX_POINT ( 'NONE', #49490 ) ;
#3413=ORIENTED_EDGE ( 'NONE', *, *, #73334, .T. ) ;
#3415=EDGE_CURVE ( 'NONE', #56310, #98903, #40039, .T. ) ;
#3416=ORIENTED_EDGE ( 'NONE', *, *, #23398, .T. ) ;
#3418=DIRECTION ( 'NONE',  ( 0.7071067811865487940, 0.7071067811865463515, 0.000000000000000000 ) ) ;
#3419=CARTESIAN_POINT ( 'NONE',  ( -16.49999999999988987, 11.52377502935401843, -1.522421517564045867 ) ) ;
#3420=CARTESIAN_POINT ( 'NONE',  ( -4.499999999999966249, 1.466399257802248446, 5.000000000000000000 ) ) ;
#3422=ORIENTED_EDGE ( 'NONE', *, *, #127631, .T. ) ;
#3423=EDGE_CURVE ( 'NONE', #14564, #105099, #61775, .T. ) ;
#3424=DIRECTION ( 'NONE',  ( 0.3543493200069163240, 0.000000000000000000, -0.9351131265310288487 ) ) ;
#3425=DIRECTION ( 'NONE',  ( -0.7071067811865487940, 0.7071067811865463515, -0.000000000000000000 ) ) ;
#3427=CARTESIAN_POINT ( 'NONE',  ( 51.29974487139158867, -27.71228299555242103, 4.000000000000000000 ) ) ;
#3429=ORIENTED_EDGE ( 'NONE', *, *, #14355, .F. ) ;
#3430=LINE ( 'NONE', #47722, #62824 ) ;
#3435=ORIENTED_EDGE ( 'NONE', *, *, #72183, .F. ) ;
#3436=FACE_OUTER_BOUND ( 'NONE', #117001, .T. ) ;
#3439=EDGE_CURVE ( 'NONE', #19849, #29105, #115372, .T. ) ;
#3441=DIRECTION ( 'NONE',  ( -0.6830127018922181881, 0.6830127018922202975, -0.2588190451025214056 ) ) ;
#3442=DIRECTION ( 'NONE',  ( -0.000000000000000000, 0.000000000000000000, 1.000000000000000000 ) ) ;
#3443=EDGE_CURVE ( 'NONE', #32886, #37230, #118247, .T. ) ;
#3444=VECTOR ( 'NONE', #8543, 1000.000000000000000 ) ;
#3445=VERTEX_POINT ( 'NONE', #50176 ) ;
#3446=ORIENTED_EDGE ( 'NONE', *, *, #77637, .T. ) ;
#3449=EDGE_LOOP ( 'NONE', ( #140842, #77799, #55185, #4550 ) ) ;
#3450=ADVANCED_FACE ( 'NONE', ( #71224 ), #7345, .F. ) ;
#3451=PLANE ( 'NONE',  #98318 ) ;
#3452=ORIENTED_EDGE ( 'NONE', *, *, #63708, .F. ) ;
#3453=AXIS2_PLACEMENT_3D ( 'NONE', #45683, #34788, #79030 ) ;
#3454=PLANE ( 'NONE',  #1977 ) ;
#3455=PLANE ( 'NONE',  #58782 ) ;
#3456=DIRECTION ( 'NONE',  ( 0.7071067811865487940, 0.7071067811865463515, -0.000000000000000000 ) ) ;
#3457=FACE_OUTER_BOUND ( 'NONE', #6258, .T. ) ;
#3458=CARTESIAN_POINT ( 'NONE',  ( -17.91685193227058548, 21.75929247661549937, 7.311836541448010429 ) ) ;
#3459=EDGE_LOOP ( 'NONE', ( #108872, #49988, #138653, #129754 ) ) ;
#3460=CARTESIAN_POINT ( 'NONE',  ( -0.005480084712502889671, 28.92564299267938210, 4.000000000000000000 ) ) ;
#3461=CARTESIAN_POINT ( 'NONE',  ( -19.56363873141800980, -2.772201803466310288, 4.368625942145798469 ) ) ;
#3462=ORIENTED_EDGE ( 'NONE', *, *, #83965, .F. ) ;
#3463=DIRECTION ( 'NONE',  ( -0.000000000000000000, 0.3543493200069153248, 0.9351131265310292928 ) ) ;
#3464=ORIENTED_EDGE ( 'NONE', *, *, #76577, .F. ) ;
#3465=ORIENTED_EDGE ( 'NONE', *, *, #56811, .F. ) ;
#3466=CARTESIAN_POINT ( 'NONE',  ( 29.99999999999979750, -2.904428200921286951, -6.989807076075011061 ) ) ;
#3467=VERTEX_POINT ( 'NONE', #82810 ) ;
#3468=EDGE_LOOP ( 'NONE', ( #62085, #26825, #34398, #39101 ) ) ;
#3469=LINE ( 'NONE', #33486, #44141 ) ;
#3470=ORIENTED_EDGE ( 'NONE', *, *, #42064, .T. ) ;
#3471=VECTOR ( 'NONE', #112670, 1000.000000000000227 ) ;
#3472=DIRECTION ( 'NONE',  ( 0.7071067811865486830, -0.7071067811865464625, -0.000000000000000000 ) ) ;
#3473=VECTOR ( 'NONE', #34375, 999.9999999999998863 ) ;
#3474=VECTOR ( 'NONE', #83611, 1000.000000000000227 ) ;
#3475=CARTESIAN_POINT ( 'NONE',  ( -10.49999999999991829, -20.94781430457062044, 5.000000000000000000 ) ) ;
#3477=FACE_OUTER_BOUND ( 'NONE', #30187, .T. ) ;
#3478=AXIS2_PLACEMENT_3D ( 'NONE', #121133, #1473, #66077 ) ;
#3479=EDGE_CURVE ( 'NONE', #97811, #21679, #139349, .T. ) ;
#3480=FACE_OUTER_BOUND ( 'NONE', #127983, .T. ) ;
#3482=DIRECTION ( 'NONE',  ( -0.7071067811865486830, -0.7071067811865464625, 0.000000000000000000 ) ) ;
#3483=ORIENTED_EDGE ( 'NONE', *, *, #35043, .T. ) ;
#3484=DIRECTION ( 'NONE',  ( -0.000000000000000000, 0.3543493200069153248, 0.9351131265310292928 ) ) ;
#3485=PLANE ( 'NONE',  #93937 ) ;
#3487=ORIENTED_EDGE ( 'NONE', *, *, #113439, .F. ) ;
#3488=LINE ( 'NONE', #48453, #81988 ) ;
#3489=EDGE_LOOP ( 'NONE', ( #43019, #127312, #43723, #106970 ) ) ;
#3490=PLANE ( 'NONE',  #132482 ) ;
#3492=ADVANCED_FACE ( 'NONE', ( #40723 ), #74057, .F. ) ;
#3493=DIRECTION ( 'NONE',  ( -0.7071067811865486830, -0.7071067811865464625, 0.000000000000000000 ) ) ;
#3494=LINE ( 'NONE', #115099, #44047 ) ;
#3496=DIRECTION ( 'NONE',  ( 0.6830127018922180770, -0.6830127018922204085, -0.2588190451025213501 ) ) ;
#3498=DIRECTION ( 'NONE',  ( 0.7071067811865487940, -0.7071067811865463515, 0.000000000000000000 ) ) ;
#3499=ADVANCED_FACE ( 'NONE', ( #87075 ), #31975, .F. ) ;
#3500=EDGE_CURVE ( 'NONE', #2711, #70215, #65355, .T. ) ;
#3502=VERTEX_POINT ( 'NONE', #131289 ) ;
#3504=ADVANCED_FACE ( 'NONE', ( #96478 ), #108069, .T. ) ;
#3505=CARTESIAN_POINT ( 'NONE',  ( -48.18398860626899705, 28.73617430169820608, 5.000000000000000000 ) ) ;
#3506=ORIENTED_EDGE ( 'NONE', *, *, #23127, .T. ) ;
#3507=EDGE_LOOP ( 'NONE', ( #107110, #73999, #127133, #68209 ) ) ;
#3508=ORIENTED_EDGE ( 'NONE', *, *, #124080, .T. ) ;
#3511=DIRECTION ( 'NONE',  ( -0.7071067811865487940, 0.7071067811865463515, -0.000000000000000000 ) ) ;
#3512=CARTESIAN_POINT ( 'NONE',  ( -45.48921356237309510, -27.52281430457087197, 5.000000000000000000 ) ) ;
#3513=VERTEX_POINT ( 'NONE', #142189 ) ;
#3514=LINE ( 'NONE', #135509, #16072 ) ;
#3515=FACE_OUTER_BOUND ( 'NONE', #90201, .T. ) ;
#3516=EDGE_CURVE ( 'NONE', #482, #51950, #64606, .T. ) ;
#3517=CARTESIAN_POINT ( 'NONE',  ( -3.183988606268992161, 28.73617430169789699, 5.000000000000000000 ) ) ;
#3518=CARTESIAN_POINT ( 'NONE',  ( 25.49999999999982236, -20.53675388469228125, 2.352720554255952834 ) ) ;
#3519=ORIENTED_EDGE ( 'NONE', *, *, #112688, .T. ) ;
#3520=EDGE_CURVE ( 'NONE', #99874, #72219, #8738, .T. ) ;
#3522=ORIENTED_EDGE ( 'NONE', *, *, #74489, .T. ) ;
#3523=VERTEX_POINT ( 'NONE', #121117 ) ;
#3524=ORIENTED_EDGE ( 'NONE', *, *, #102074, .T. ) ;
#3525=PLANE ( 'NONE',  #63265 ) ;
#3527=ADVANCED_FACE ( 'NONE', ( #63906 ), #108781, .F. ) ;
#3528=ORIENTED_EDGE ( 'NONE', *, *, #10192, .T. ) ;
#3530=ADVANCED_FACE ( 'NONE', ( #9474 ), #88517, .F. ) ;
#3533=DIRECTION ( 'NONE',  ( 0.7071067811865486830, 0.7071067811865464625, 0.000000000000000000 ) ) ;
#3534=VECTOR ( 'NONE', #89551, 1000.000000000000000 ) ;
#3536=DIRECTION ( 'NONE',  ( -0.000000000000000000, -0.3543493200069152693, 0.9351131265310292928 ) ) ;
#3538=LINE ( 'NONE', #35533, #20781 ) ;
#3539=VECTOR ( 'NONE', #87444, 1000.000000000000000 ) ;
#3540=LINE ( 'NONE', #83854, #32492 ) ;
#3541=CARTESIAN_POINT ( 'NONE',  ( 21.48921356237309155, -27.52281430457070499, 5.000000000000000000 ) ) ;
#3542=CARTESIAN_POINT ( 'NONE',  ( 2.669897814527331992, 17.25929247661554555, 19.83885114516070658 ) ) ;
#3543=EDGE_CURVE ( 'NONE', #26060, #96265, #53752, .T. ) ;
#3544=DIRECTION ( 'NONE',  ( 0.7071067811865487940, 0.7071067811865463515, -0.000000000000000000 ) ) ;
#3546=LINE ( 'NONE', #47153, #21346 ) ;
#3547=DIRECTION ( 'NONE',  ( -0.000000000000000000, 0.3543493200069153248, 0.9351131265310292928 ) ) ;
#3548=CARTESIAN_POINT ( 'NONE',  ( 69.18398860626899705, 28.73617430169835529, 5.000000000000000000 ) ) ;
#3549=DIRECTION ( 'NONE',  ( -0.3543493200069162685, -0.000000000000000000, -0.9351131265310288487 ) ) ;
#3550=ORIENTED_EDGE ( 'NONE', *, *, #103057, .T. ) ;
#3552=ORIENTED_EDGE ( 'NONE', *, *, #92910, .F. ) ;
#3553=ADVANCED_FACE ( 'NONE', ( #86378 ), #32712, .F. ) ;
#3555=VERTEX_POINT ( 'NONE', #110222 ) ;
#3556=VECTOR ( 'NONE', #133918, 1000.000000000000000 ) ;
#3557=ORIENTED_EDGE ( 'NONE', *, *, #22856, .F. ) ;
#3559=DIRECTION ( 'NONE',  ( 0.3543493200069164351, 2.781805975412904658E-17, -0.9351131265310288487 ) ) ;
#3561=VERTEX_POINT ( 'NONE', #55167 ) ;
#3562=CARTESIAN_POINT ( 'NONE',  ( 45.18398860626900415, 28.73617430169818832, 5.000000000000000000 ) ) ;
#3563=ADVANCED_FACE ( 'NONE', ( #9 ), #121815, .T. ) ;
#3564=DIRECTION ( 'NONE',  ( -0.7071067811865486830, 0.7071067811865464625, 0.000000000000000000 ) ) ;
#3565=FACE_OUTER_BOUND ( 'NONE', #48736, .T. ) ;
#3567=EDGE_CURVE ( 'NONE', #105583, #51106, #11610, .T. ) ;
#3568=DIRECTION ( 'NONE',  ( 0.7071067811865487940, 0.7071067811865463515, 0.000000000000000000 ) ) ;
#3569=LINE ( 'NONE', #125395, #58998 ) ;
#3570=CARTESIAN_POINT ( 'NONE',  ( 66.29974487139159578, -27.71228299555252406, 4.000000000000000000 ) ) ;
#3571=CARTESIAN_POINT ( 'NONE',  ( 12.70710678118645731, 2.259292476615688994, 5.000000000000000000 ) ) ;
#3572=CARTESIAN_POINT ( 'NONE',  ( 0.000000000000000000, -4.068876922607777225, 4.000000000000000000 ) ) ;
#3573=CARTESIAN_POINT ( 'NONE',  ( 33.48921356237309510, -27.52281430457078670, 5.000000000000000000 ) ) ;
#3575=AXIS2_PLACEMENT_3D ( 'NONE', #28221, #39836, #84056 ) ;
#3576=PLANE ( 'NONE',  #70091 ) ;
#3577=EDGE_LOOP ( 'NONE', ( #118759, #87844, #72553, #94416 ) ) ;
#3578=ORIENTED_EDGE ( 'NONE', *, *, #45322, .T. ) ;
#3579=VECTOR ( 'NONE', #103608, 1000.000000000000000 ) ;
#3581=ORIENTED_EDGE ( 'NONE', *, *, #128326, .T. ) ;
#3583=EDGE_CURVE ( 'NONE', #112964, #38224, #45043, .T. ) ;
#3584=LINE ( 'NONE', #25359, #133526 ) ;
#3585=VECTOR ( 'NONE', #94657, 999.9999999999998863 ) ;
#3587=ORIENTED_EDGE ( 'NONE', *, *, #88857, .T. ) ;
#3588=EDGE_CURVE ( 'NONE', #71830, #138961, #67493, .T. ) ;
#3589=CARTESIAN_POINT ( 'NONE',  ( 3.299744871391591339, -27.71228299555208352, 4.000000000000000000 ) ) ;
#3592=VERTEX_POINT ( 'NONE', #100095 ) ;
#3594=CARTESIAN_POINT ( 'NONE',  ( -6.938893903907228378E-15, -2.904428200921318481, -6.989807076074944447 ) ) ;
#3595=CARTESIAN_POINT ( 'NONE',  ( 21.00548008471250938, 28.92564299267923644, 4.000000000000000000 ) ) ;
#3596=ORIENTED_EDGE ( 'NONE', *, *, #125546, .T. ) ;
#3597=ORIENTED_EDGE ( 'NONE', *, *, #69066, .T. ) ;
#3598=VERTEX_POINT ( 'NONE', #748 ) ;
#3599=CARTESIAN_POINT ( 'NONE',  ( -8.510786437626906675, -27.52281430457049183, 5.000000000000000000 ) ) ;
#3605=ORIENTED_EDGE ( 'NONE', *, *, #130130, .F. ) ;
#3606=PLANE ( 'NONE',  #96492 ) ;
#3607=ORIENTED_EDGE ( 'NONE', *, *, #43777, .T. ) ;
#3608=ORIENTED_EDGE ( 'NONE', *, *, #8739, .T. ) ;
#3609=CARTESIAN_POINT ( 'NONE',  ( 5.816011393731002066, 28.73617430169783304, 5.000000000000000000 ) ) ;
#3610=CARTESIAN_POINT ( 'NONE',  ( 14.99999999999990585, 8.966399257802175171, 5.000000000000000000 ) ) ;
#3611=CARTESIAN_POINT ( 'NONE',  ( 21.29974487139158512, -27.71228299555221142, 4.000000000000000000 ) ) ;
#3612=ORIENTED_EDGE ( 'NONE', *, *, #62969, .F. ) ;
#3613=LINE ( 'NONE', #89933, #78410 ) ;
#3614=DIRECTION ( 'NONE',  ( -0.3543493200069162685, -0.000000000000000000, -0.9351131265310288487 ) ) ;
#3615=FACE_OUTER_BOUND ( 'NONE', #1981, .T. ) ;
#3616=FACE_BOUND ( 'NONE', #97068, .T. ) ;
#3617=ORIENTED_EDGE ( 'NONE', *, *, #100811, .T. ) ;
#3618=DIRECTION ( 'NONE',  ( -0.7071067811865486830, 0.7071067811865463515, 0.000000000000000000 ) ) ;
#3619=CARTESIAN_POINT ( 'NONE',  ( -9.328169399223467551, 2.259292476615694323, 4.000000000000000000 ) ) ;
#3621=ORIENTED_EDGE ( 'NONE', *, *, #55103, .F. ) ;
#3622=CARTESIAN_POINT ( 'NONE',  ( -7.499999999999951150, 22.08746187583901843, 4.000000000000000000 ) ) ;
#3624=ORIENTED_EDGE ( 'NONE', *, *, #27023, .F. ) ;
#3625=ORIENTED_EDGE ( 'NONE', *, *, #119590, .T. ) ;
#3626=VECTOR ( 'NONE', #47198, 1000.000000000000000 ) ;
#3628=EDGE_LOOP ( 'NONE', ( #29084, #54341, #126120, #87490 ) ) ;
#3629=CARTESIAN_POINT ( 'NONE',  ( -42.48921356237308800, -27.52281430457085065, 5.000000000000000000 ) ) ;
#3630=VECTOR ( 'NONE', #35045, 1000.000000000000227 ) ;
#3631=DIRECTION ( 'NONE',  ( 1.000000000000000000, 0.000000000000000000, 0.000000000000000000 ) ) ;
#3632=LINE ( 'NONE', #102995, #10260 ) ;
#3634=ADVANCED_FACE ( 'NONE', ( #38023 ), #73498, .T. ) ;
#3635=CARTESIAN_POINT ( 'NONE',  ( 8.816011393731004731, 28.73617430169781173, 5.000000000000000000 ) ) ;
#3636=CARTESIAN_POINT ( 'NONE',  ( -35.99451991528749772, 28.92564299267963079, 4.000000000000000000 ) ) ;
#3637=PLANE ( 'NONE',  #57535 ) ;
#3638=DIRECTION ( 'NONE',  ( -0.7071067811865486830, 0.7071067811865464625, 0.000000000000000000 ) ) ;
#3639=VECTOR ( 'NONE', #8864, 999.9999999999998863 ) ;
#3640=EDGE_CURVE ( 'NONE', #10027, #73248, #115310, .T. ) ;
#3641=ORIENTED_EDGE ( 'NONE', *, *, #73765, .F. ) ;
#3642=ORIENTED_EDGE ( 'NONE', *, *, #72735, .F. ) ;
#3643=ORIENTED_EDGE ( 'NONE', *, *, #66682, .F. ) ;
#3644=ORIENTED_EDGE ( 'NONE', *, *, #33729, .F. ) ;
#3645=ORIENTED_EDGE ( 'NONE', *, *, #66822, .T. ) ;
#3646=ADVANCED_FACE ( 'NONE', ( #117662 ), #29963, .T. ) ;
#3647=VERTEX_POINT ( 'NONE', #118399 ) ;
#3648=CARTESIAN_POINT ( 'NONE',  ( -8.999999999999934275, -1.447814304570815169, 5.000000000000000000 ) ) ;
#3649=DIRECTION ( 'NONE',  ( -1.000000000000000000, 5.151277200819050839E-14, 0.000000000000000000 ) ) ;
#3650=EDGE_CURVE ( 'NONE', #133870, #54574, #139497, .T. ) ;
#3651=EDGE_CURVE ( 'NONE', #97655, #122495, #40180, .T. ) ;
#3653=ORIENTED_EDGE ( 'NONE', *, *, #99913, .F. ) ;
#3655=EDGE_LOOP ( 'NONE', ( #129888, #120836, #26462, #126212 ) ) ;
#3656=VECTOR ( 'NONE', #104884, 1000.000000000000227 ) ;
#3658=EDGE_CURVE ( 'NONE', #34174, #20152, #84390, .T. ) ;
#3659=EDGE_CURVE ( 'NONE', #6418, #75592, #115514, .T. ) ;
#3661=VECTOR ( 'NONE', #6772, 1000.000000000000000 ) ;
#3663=VERTEX_POINT ( 'NONE', #27834 ) ;
#3665=CYLINDRICAL_SURFACE ( 'NONE', #70793, 0.5000000000000004441 ) ;
#3667=EDGE_CURVE ( 'NONE', #17718, #84184, #113400, .T. ) ;
#3670=ORIENTED_EDGE ( 'NONE', *, *, #36206, .F. ) ;
#3671=EDGE_LOOP ( 'NONE', ( #129027, #58220, #39192, #50932 ) ) ;
#3672=DIRECTION ( 'NONE',  ( 0.6830127018922181881, 0.6830127018922202975, -0.2588190451025214056 ) ) ;
#3673=ORIENTED_EDGE ( 'NONE', *, *, #66100, .F. ) ;
#3674=LINE ( 'NONE', #93587, #44049 ) ;
#3675=PLANE ( 'NONE',  #34828 ) ;
#3676=DIRECTION ( 'NONE',  ( -0.000000000000000000, -0.3543493200069152693, 0.9351131265310292928 ) ) ;
#3678=DIRECTION ( 'NONE',  ( -0.000000000000000000, 0.3543493200069153248, 0.9351131265310292928 ) ) ;
#3679=ORIENTED_EDGE ( 'NONE', *, *, #89408, .T. ) ;
#3680=DIRECTION ( 'NONE',  ( 0.7071067811865487940, 0.7071067811865463515, 0.000000000000000000 ) ) ;
#3681=ADVANCED_FACE ( 'NONE', ( #85069 ), #49630, .F. ) ;
#3682=DIRECTION ( 'NONE',  ( -0.7071067811865486830, 0.7071067811865464625, 0.000000000000000000 ) ) ;
#3683=CARTESIAN_POINT ( 'NONE',  ( -63.18398860626900415, 28.73617430169831621, 5.000000000000000000 ) ) ;
#3684=ORIENTED_EDGE ( 'NONE', *, *, #54317, .F. ) ;
#3685=PLANE ( 'NONE',  #30446 ) ;
#3687=ORIENTED_EDGE ( 'NONE', *, *, #3987, .F. ) ;
#3688=CARTESIAN_POINT ( 'NONE',  ( 36.18398860626899705, 28.73617430169812437, 5.000000000000000000 ) ) ;
#3689=ORIENTED_EDGE ( 'NONE', *, *, #65043, .T. ) ;
#3691=LINE ( 'NONE', #139276, #137332 ) ;
#3692=DIRECTION ( 'NONE',  ( 0.7071067811865487940, 0.7071067811865463515, 0.000000000000000000 ) ) ;
#3694=ORIENTED_EDGE ( 'NONE', *, *, #14525, .F. ) ;
#3696=PLANE ( 'NONE',  #90098 ) ;
#3699=LINE ( 'NONE', #90026, #72163 ) ;
#3700=PLANE ( 'NONE',  #56025 ) ;
#3701=EDGE_CURVE ( 'NONE', #121450, #116985, #105384, .T. ) ;
#3706=CARTESIAN_POINT ( 'NONE',  ( -11.29289321881337216, 5.259292476615661016, 5.000000000000000000 ) ) ;
#3708=ORIENTED_EDGE ( 'NONE', *, *, #22336, .T. ) ;
#3709=VERTEX_POINT ( 'NONE', #93806 ) ;
#3710=EDGE_CURVE ( 'NONE', #68343, #76248, #6040, .T. ) ;
#3712=EDGE_LOOP ( 'NONE', ( #62944, #26907, #113600, #140208 ) ) ;
#3714=ADVANCED_FACE ( 'NONE', ( #138756 ), #50316, .F. ) ;
#3715=ORIENTED_EDGE ( 'NONE', *, *, #29440, .F. ) ;
#3717=DIRECTION ( 'NONE',  ( -0.000000000000000000, 0.3543493200069153248, 0.9351131265310292928 ) ) ;
#3719=ORIENTED_EDGE ( 'NONE', *, *, #46344, .F. ) ;
#3720=PLANE ( 'NONE',  #124897 ) ;
#3721=EDGE_CURVE ( 'NONE', #79129, #87604, #38720, .T. ) ;
#3725=ORIENTED_EDGE ( 'NONE', *, *, #105591, .F. ) ;
#3726=LINE ( 'NONE', #15325, #53379 ) ;
#3727=LINE ( 'NONE', #48018, #37733 ) ;
#3730=CARTESIAN_POINT ( 'NONE',  ( 5.700255128608413102, -27.71228299555201957, 4.000000000000000000 ) ) ;
#3732=LINE ( 'NONE', #92193, #141822 ) ;
#3733=CARTESIAN_POINT ( 'NONE',  ( -21.18398860626899349, 28.73617430169802134, 5.000000000000000000 ) ) ;
#3735=VECTOR ( 'NONE', #101912, 1000.000000000000227 ) ;
#3736=DIRECTION ( 'NONE',  ( 0.7071067811865487940, 0.7071067811865463515, 0.000000000000000000 ) ) ;
#3738=ORIENTED_EDGE ( 'NONE', *, *, #9128, .T. ) ;
#3739=ORIENTED_EDGE ( 'NONE', *, *, #41354, .F. ) ;
#3741=ORIENTED_EDGE ( 'NONE', *, *, #43777, .F. ) ;
#3742=VECTOR ( 'NONE', #4108, 999.9999999999998863 ) ;
#3743=EDGE_LOOP ( 'NONE', ( #50089, #133570, #125348, #98410 ) ) ;
#3744=ADVANCED_FACE ( 'NONE', ( #143023 ), #31415, .F. ) ;
#3745=CARTESIAN_POINT ( 'NONE',  ( 32.99999999999977973, 8.587461875839167647, 4.000000000000000000 ) ) ;
#3747=EDGE_LOOP ( 'NONE', ( #34545, #33508, #91184, #83687 ) ) ;
#3748=LINE ( 'NONE', #26268, #31656 ) ;
#3749=DIRECTION ( 'NONE',  ( 0.7071067811865487940, 0.7071067811865463515, 0.000000000000000000 ) ) ;
#3750=LINE ( 'NONE', #37134, #95303 ) ;
#3753=DIRECTION ( 'NONE',  ( -0.7071067811865486830, -0.7071067811865464625, -0.000000000000000000 ) ) ;
#3754=ORIENTED_EDGE ( 'NONE', *, *, #118260, .T. ) ;
#3755=CARTESIAN_POINT ( 'NONE',  ( 0.000000000000000000, 7.588810512006213038, -3.013526669885226994 ) ) ;
#3758=DIRECTION ( 'NONE',  ( -0.7071067811865486830, -0.7071067811865464625, 0.000000000000000000 ) ) ;
#3759=EDGE_LOOP ( 'NONE', ( #136935, #2662, #111618, #92744 ) ) ;
#3760=EDGE_CURVE ( 'NONE', #100040, #99958, #64754, .T. ) ;
#3761=AXIS2_PLACEMENT_3D ( 'NONE', #89740, #111490, #134706 ) ;
#3762=VERTEX_POINT ( 'NONE', #21949 ) ;
#3763=DIRECTION ( 'NONE',  ( -0.000000000000000000, 0.3543493200069153248, 0.9351131265310292928 ) ) ;
#3764=LINE ( 'NONE', #16068, #41581 ) ;
#3765=CARTESIAN_POINT ( 'NONE',  ( 8.999999999999932498, -22.22500000000000853, 4.412002311790025999 ) ) ;
#3766=VECTOR ( 'NONE', #62654, 999.9999999999998863 ) ;
#3767=VECTOR ( 'NONE', #82133, 1000.000000000000000 ) ;
#3770=CARTESIAN_POINT ( 'NONE',  ( 9.328169399223463998, -3.740707523384244837, 4.000000000000000000 ) ) ;
#3771=CARTESIAN_POINT ( 'NONE',  ( 60.18398860626900415, 28.73617430169829490, 5.000000000000000000 ) ) ;
#3772=VERTEX_POINT ( 'NONE', #120515 ) ;
#3773=ORIENTED_EDGE ( 'NONE', *, *, #117751, .F. ) ;
#3774=VECTOR ( 'NONE', #60868, 1000.000000000000227 ) ;
#3775=CARTESIAN_POINT ( 'NONE',  ( -6.183988606268994381, 28.73617430169791476, 5.000000000000000000 ) ) ;
#3776=ORIENTED_EDGE ( 'NONE', *, *, #112393, .F. ) ;
#3777=EDGE_CURVE ( 'NONE', #121813, #70885, #43710, .T. ) ;
#3778=EDGE_CURVE ( 'NONE', #108671, #42790, #8871, .T. ) ;
#3779=CARTESIAN_POINT ( 'NONE',  ( -28.82816939922333432, 12.75929247661558996, 4.000000000000000000 ) ) ;
#3780=ORIENTED_EDGE ( 'NONE', *, *, #86903, .F. ) ;
#3781=DIRECTION ( 'NONE',  ( 0.7071067811865487940, -0.7071067811865463515, 0.000000000000000000 ) ) ;
#3782=DIRECTION ( 'NONE',  ( 0.7071067811865487940, -0.7071067811865463515, -0.000000000000000000 ) ) ;
#3783=FACE_BOUND ( 'NONE', #18436, .T. ) ;
#3784=EDGE_CURVE ( 'NONE', #44987, #45460, #96618, .T. ) ;
#3785=DIRECTION ( 'NONE',  ( -0.3543493200069162685, -0.000000000000000000, -0.9351131265310288487 ) ) ;
#3787=CARTESIAN_POINT ( 'NONE',  ( -32.99999999999977263, 19.93112307739198386, 4.000000000000000000 ) ) ;
#3789=CARTESIAN_POINT ( 'NONE',  ( 1.499999999999987566, -14.70932175296477062, -11.46312253303837636 ) ) ;
#3790=ORIENTED_EDGE ( 'NONE', *, *, #97733, .T. ) ;
#3791=CARTESIAN_POINT ( 'NONE',  ( 26.99999999999982236, -19.44781430457063465, 5.000000000000000000 ) ) ;
#3792=ORIENTED_EDGE ( 'NONE', *, *, #141574, .F. ) ;
#3793=ORIENTED_EDGE ( 'NONE', *, *, #23027, .T. ) ;
#3797=CARTESIAN_POINT ( 'NONE',  ( 30.48921356237309510, -27.52281430457076894, 5.000000000000000000 ) ) ;
#3798=ORIENTED_EDGE ( 'NONE', *, *, #42342, .F. ) ;
#3800=AXIS2_PLACEMENT_3D ( 'NONE', #112391, #58040, #135580 ) ;
#3802=CARTESIAN_POINT ( 'NONE',  ( -24.48921356237309510, -27.52281430457072631, 5.000000000000000000 ) ) ;
#3803=DIRECTION ( 'NONE',  ( -0.6830127018922181881, 0.6830127018922202975, -0.2588190451025214056 ) ) ;
#3804=CARTESIAN_POINT ( 'NONE',  ( -33.29974487139158867, -27.71228299555229313, 4.000000000000000000 ) ) ;
#3805=FACE_OUTER_BOUND ( 'NONE', #56449, .T. ) ;
#3806=CARTESIAN_POINT ( 'NONE',  ( 29.34328999833768847, 3.759292476615678336, 13.27625715073272517 ) ) ;
#3807=DIRECTION ( 'NONE',  ( 1.000000000000000000, 0.000000000000000000, 0.000000000000000000 ) ) ;
#3808=ORIENTED_EDGE ( 'NONE', *, *, #46123, .F. ) ;
#3810=VERTEX_POINT ( 'NONE', #9627 ) ;
#3811=CARTESIAN_POINT ( 'NONE',  ( -48.18398860626899705, 28.73617430169820608, 5.000000000000000000 ) ) ;
#3812=CARTESIAN_POINT ( 'NONE',  ( 0.000000000000000000, 0.000000000000000000, 5.000000000000000000 ) ) ;
#3813=ORIENTED_EDGE ( 'NONE', *, *, #31879, .T. ) ;
#3814=ORIENTED_EDGE ( 'NONE', *, *, #63147, .T. ) ;
#3815=ORIENTED_EDGE ( 'NONE', *, *, #31375, .T. ) ;
#3817=EDGE_CURVE ( 'NONE', #109916, #91920, #86519, .T. ) ;
#3818=CARTESIAN_POINT ( 'NONE',  ( 30.48921356237309510, -27.52281430457076894, 5.000000000000000000 ) ) ;
#3819=ORIENTED_EDGE ( 'NONE', *, *, #105571, .T. ) ;
#3820=LINE ( 'NONE', #105318, #104191 ) ;
#3823=EDGE_CURVE ( 'NONE', #58068, #22022, #140858, .T. ) ;
#3825=CARTESIAN_POINT ( 'NONE',  ( -7.499999999999945821, 12.05218569542904561, 5.000000000000000000 ) ) ;
#3827=ORIENTED_EDGE ( 'NONE', *, *, #24964, .F. ) ;
#3828=AXIS2_PLACEMENT_3D ( 'NONE', #103299, #37359, #81594 ) ;
#3829=LINE ( 'NONE', #36512, #91993 ) ;
#3833=DIRECTION ( 'NONE',  ( 0.3543493200069162685, -0.000000000000000000, -0.9351131265310288487 ) ) ;
#3834=VERTEX_POINT ( 'NONE', #43012 ) ;
#3835=ORIENTED_EDGE ( 'NONE', *, *, #24367, .T. ) ;
#3836=EDGE_CURVE ( 'NONE', #66460, #6035, #21242, .T. ) ;
#3837=CARTESIAN_POINT ( 'NONE',  ( 3.183988606268992161, 28.73617430169789699, 5.000000000000000000 ) ) ;
#3838=DIRECTION ( 'NONE',  ( -0.000000000000000000, 0.3543493200069153248, 0.9351131265310292928 ) ) ;
#3840=EDGE_LOOP ( 'NONE', ( #137749, #121038, #124948, #32635 ) ) ;
#3841=CARTESIAN_POINT ( 'NONE',  ( -5.999999999999963585, 20.70535890316560668, 1.956823837851930481 ) ) ;
#3842=DIRECTION ( 'NONE',  ( -0.7071067811865486830, -0.7071067811865464625, -0.000000000000000000 ) ) ;
#3845=PLANE ( 'NONE',  #51188 ) ;
#3846=LINE ( 'NONE', #48130, #9724 ) ;
#3847=ORIENTED_EDGE ( 'NONE', *, *, #1702, .T. ) ;
#3848=CARTESIAN_POINT ( 'NONE',  ( 33.48921356237309510, -27.52281430457078670, 5.000000000000000000 ) ) ;
#3849=LINE ( 'NONE', #48133, #137313 ) ;
#3850=LINE ( 'NONE', #114775, #30689 ) ;
#3852=CARTESIAN_POINT ( 'NONE',  ( 0.000000000000000000, 10.93112307739207978, 4.000000000000000000 ) ) ;
#3855=EDGE_CURVE ( 'NONE', #7505, #43144, #90055, .T. ) ;
#3856=ORIENTED_EDGE ( 'NONE', *, *, #143155, .F. ) ;
#3857=ORIENTED_EDGE ( 'NONE', *, *, #130066, .F. ) ;
#3858=CARTESIAN_POINT ( 'NONE',  ( 32.16170612452599897, -6.740707523384223521, 16.75550250614875480 ) ) ;
#3859=DIRECTION ( 'NONE',  ( 1.000000000000000000, 0.000000000000000000, 0.000000000000000000 ) ) ;
#3860=EDGE_CURVE ( 'NONE', #12969, #57857, #45180, .T. ) ;
#3862=AXIS2_PLACEMENT_3D ( 'NONE', #134908, #25378, #81229 ) ;
#3864=LINE ( 'NONE', #80084, #13419 ) ;
#3865=AXIS2_PLACEMENT_3D ( 'NONE', #51228, #83133, #95423 ) ;
#3866=LINE ( 'NONE', #5318, #138742 ) ;
#3867=DIRECTION ( 'NONE',  ( 0.000000000000000000, -0.3543493200069152138, 0.9351131265310292928 ) ) ;
#3868=CARTESIAN_POINT ( 'NONE',  ( 30.48921356237309510, -27.52281430457076894, 5.000000000000000000 ) ) ;
#3869=VERTEX_POINT ( 'NONE', #133588 ) ;
#3870=DIRECTION ( 'NONE',  ( 1.000000000000000000, 0.000000000000000000, 0.000000000000000000 ) ) ;
#3871=AXIS2_PLACEMENT_3D ( 'NONE', #23770, #133952, #45551 ) ;
#3872=CARTESIAN_POINT ( 'NONE',  ( 36.18398860626899705, 28.73617430169812437, 5.000000000000000000 ) ) ;
#3873=VECTOR ( 'NONE', #6598, 1000.000000000000000 ) ;
#3874=CARTESIAN_POINT ( 'NONE',  ( -14.51078643762690490, -27.52281430457045275, 5.000000000000000000 ) ) ;
#3876=DIRECTION ( 'NONE',  ( -0.7071067811865486830, -0.7071067811865464625, 0.000000000000000000 ) ) ;
#3877=CARTESIAN_POINT ( 'NONE',  ( -6.183988606268994381, 28.73617430169791476, 5.000000000000000000 ) ) ;
#3878=ORIENTED_EDGE ( 'NONE', *, *, #99618, .F. ) ;
#3879=CARTESIAN_POINT ( 'NONE',  ( 18.70710678118641468, -12.74070752338415247, 5.000000000000000000 ) ) ;
#3880=EDGE_CURVE ( 'NONE', #96580, #31310, #34268, .T. ) ;
#3881=EDGE_LOOP ( 'NONE', ( #60027, #47426, #63642, #119578 ) ) ;
#3882=DIRECTION ( 'NONE',  ( -0.7071067811865487940, 0.7071067811865463515, -0.000000000000000000 ) ) ;
#3884=FACE_OUTER_BOUND ( 'NONE', #74681, .T. ) ;
#3885=DIRECTION ( 'NONE',  ( -0.7071067811865487940, 0.7071067811865463515, 0.000000000000000000 ) ) ;
#3886=DIRECTION ( 'NONE',  ( 0.7071067811865486830, -0.7071067811865464625, -0.000000000000000000 ) ) ;
#3887=DIRECTION ( 'NONE',  ( -0.7071067811865486830, -0.7071067811865464625, 0.000000000000000000 ) ) ;
#3888=VERTEX_POINT ( 'NONE', #23370 ) ;
#3889=FACE_OUTER_BOUND ( 'NONE', #107226, .T. ) ;
#3890=CARTESIAN_POINT ( 'NONE',  ( -13.49999999999990052, -7.912538124160676922, 4.000000000000000000 ) ) ;
#3892=AXIS2_PLACEMENT_3D ( 'NONE', #74870, #19729, #21875 ) ;
#3893=CARTESIAN_POINT ( 'NONE',  ( -28.99806943317882002, -22.22500000000000142, 4.500000000000000888 ) ) ;
#3894=EDGE_CURVE ( 'NONE', #122495, #91285, #14655, .T. ) ;
#3897=AXIS2_PLACEMENT_3D ( 'NONE', #57590, #101773, #135157 ) ;
#3898=CARTESIAN_POINT ( 'NONE',  ( 36.29974487139159578, -27.71228299555231445, 4.000000000000000000 ) ) ;
#3899=ORIENTED_EDGE ( 'NONE', *, *, #125868, .F. ) ;
#3900=ORIENTED_EDGE ( 'NONE', *, *, #19303, .T. ) ;
#3902=FACE_OUTER_BOUND ( 'NONE', #3671, .T. ) ;
#3904=PLANE ( 'NONE',  #90233 ) ;
#3905=LINE ( 'NONE', #115526, #135466 ) ;
#3907=ORIENTED_EDGE ( 'NONE', *, *, #45178, .T. ) ;
#3908=CARTESIAN_POINT ( 'NONE',  ( 6.707106781186499944, -9.740707523384186217, 5.000000000000000000 ) ) ;
#3909=EDGE_CURVE ( 'NONE', #98989, #50205, #100937, .T. ) ;
#3912=LINE ( 'NONE', #27136, #34436 ) ;
#3914=ORIENTED_EDGE ( 'NONE', *, *, #47579, .F. ) ;
#3915=CARTESIAN_POINT ( 'NONE',  ( -20.99999999999985789, 19.93112307739198386, 4.000000000000000000 ) ) ;
#3916=CARTESIAN_POINT ( 'NONE',  ( -13.49999999999991473, 13.08746187583912146, 4.000000000000000000 ) ) ;
#3917=VECTOR ( 'NONE', #94749, 1000.000000000000227 ) ;
#3918=LINE ( 'NONE', #45375, #48621 ) ;
#3919=EDGE_CURVE ( 'NONE', #140124, #103327, #24108, .T. ) ;
#3920=CARTESIAN_POINT ( 'NONE',  ( -36.48921356237310221, -27.52281430457080802, 5.000000000000000000 ) ) ;
#3921=CARTESIAN_POINT ( 'NONE',  ( -5.816011393731002066, 28.73617430169783304, 5.000000000000000000 ) ) ;
#3922=VERTEX_POINT ( 'NONE', #68362 ) ;
#3923=DIRECTION ( 'NONE',  ( 0.6830127018922180770, -0.6830127018922204085, -0.2588190451025213501 ) ) ;
#3924=CARTESIAN_POINT ( 'NONE',  ( -36.49816348513933661, -17.24070752338410628, 8.407044977365309535 ) ) ;
#3926=DIRECTION ( 'NONE',  ( 0.7071067811865486830, -0.7071067811865464625, -0.000000000000000000 ) ) ;
#3927=ORIENTED_EDGE ( 'NONE', *, *, #143472, .T. ) ;
#3928=EDGE_CURVE ( 'NONE', #117254, #13095, #24805, .T. ) ;
#3929=ORIENTED_EDGE ( 'NONE', *, *, #34878, .T. ) ;
#3931=LINE ( 'NONE', #81578, #76552 ) ;
#3932=LINE ( 'NONE', #94544, #80348 ) ;
#3933=DIRECTION ( 'NONE',  ( -0.6830127018922181881, 0.6830127018922202975, -0.2588190451025214056 ) ) ;
#3934=CARTESIAN_POINT ( 'NONE',  ( 8.999999999999937828, 7.931123077392104648, 4.000000000000000000 ) ) ;
#3935=ORIENTED_EDGE ( 'NONE', *, *, #59123, .T. ) ;
#3936=VERTEX_POINT ( 'NONE', #48719 ) ;
#3937=CARTESIAN_POINT ( 'NONE',  ( 8.999999999999941380, -12.03360074219761700, 5.000000000000000000 ) ) ;
#3938=DIRECTION ( 'NONE',  ( 0.7071067811865487940, 0.7071067811865463515, 0.000000000000000000 ) ) ;
#3939=ORIENTED_EDGE ( 'NONE', *, *, #82209, .T. ) ;
#3940=ADVANCED_FACE ( 'NONE', ( #59612 ), #137156, .F. ) ;
#3942=ORIENTED_EDGE ( 'NONE', *, *, #16365, .F. ) ;
#3943=DIRECTION ( 'NONE',  ( 1.000000000000000000, 0.000000000000000000, 0.000000000000000000 ) ) ;
#3944=LINE ( 'NONE', #92414, #114151 ) ;
#3945=AXIS2_PLACEMENT_3D ( 'NONE', #126826, #22675, #34310 ) ;
#3946=FACE_BOUND ( 'NONE', #24047, .T. ) ;
#3947=EDGE_CURVE ( 'NONE', #139810, #88227, #106625, .T. ) ;
#3949=FACE_OUTER_BOUND ( 'NONE', #8694, .T. ) ;
#3950=CARTESIAN_POINT ( 'NONE',  ( 0.000000000000000000, 0.000000000000000000, 5.000000000000000000 ) ) ;
#3951=CARTESIAN_POINT ( 'NONE',  ( -66.48921356237309510, -27.52281430457101763, 5.000000000000000000 ) ) ;
#3952=AXIS2_PLACEMENT_3D ( 'NONE', #100993, #77832, #111887 ) ;
#3953=AXIS2_PLACEMENT_3D ( 'NONE', #130436, #31126, #32544 ) ;
#3954=VECTOR ( 'NONE', #135042, 1000.000000000000227 ) ;
#3955=ORIENTED_EDGE ( 'NONE', *, *, #15196, .T. ) ;
#3956=AXIS2_PLACEMENT_3D ( 'NONE', #136991, #46456, #103618 ) ;
#3957=ORIENTED_EDGE ( 'NONE', *, *, #115566, .T. ) ;
#3959=VERTEX_POINT ( 'NONE', #83498 ) ;
#3960=LINE ( 'NONE', #123687, #35079 ) ;
#3961=VECTOR ( 'NONE', #18954, 999.9999999999998863 ) ;
#3962=CARTESIAN_POINT ( 'NONE',  ( -51.48921356237309510, -27.52281430457091460, 5.000000000000000000 ) ) ;
#3963=DIRECTION ( 'NONE',  ( 0.3543493200069162685, -0.000000000000000000, -0.9351131265310288487 ) ) ;
#3965=FACE_OUTER_BOUND ( 'NONE', #119508, .T. ) ;
#3968=LINE ( 'NONE', #69303, #17275 ) ;
#3969=DIRECTION ( 'NONE',  ( -0.000000000000000000, -0.3543493200069152693, 0.9351131265310292928 ) ) ;
#3970=PLANE ( 'NONE',  #72259 ) ;
#3971=VERTEX_POINT ( 'NONE', #95051 ) ;
#3973=CARTESIAN_POINT ( 'NONE',  ( 12.29974487139158512, -27.71228299555214747, 4.000000000000000000 ) ) ;
#3974=ORIENTED_EDGE ( 'NONE', *, *, #100908, .F. ) ;
#3975=ORIENTED_EDGE ( 'NONE', *, *, #136004, .F. ) ;
#3976=ORIENTED_EDGE ( 'NONE', *, *, #113381, .F. ) ;
#3978=VECTOR ( 'NONE', #102503, 1000.000000000000000 ) ;
#3979=ORIENTED_EDGE ( 'NONE', *, *, #79015, .T. ) ;
#3984=EDGE_LOOP ( 'NONE', ( #27200, #68259, #9378, #62061 ) ) ;
#3985=EDGE_CURVE ( 'NONE', #19842, #22107, #71925, .T. ) ;
#3987=EDGE_CURVE ( 'NONE', #73784, #105152, #72657, .T. ) ;
#3988=ORIENTED_EDGE ( 'NONE', *, *, #120443, .T. ) ;
#3989=PLANE ( 'NONE',  #139044 ) ;
#3991=CARTESIAN_POINT ( 'NONE',  ( 15.29974487139158867, -27.71228299555216879, 4.000000000000000000 ) ) ;
#3992=PLANE ( 'NONE',  #97974 ) ;
#3993=ORIENTED_EDGE ( 'NONE', *, *, #141672, .F. ) ;
#3994=VERTEX_POINT ( 'NONE', #40700 ) ;
#3995=EDGE_CURVE ( 'NONE', #24646, #76671, #16791, .T. ) ;
#3996=PLANE ( 'NONE',  #113983 ) ;
#3997=CARTESIAN_POINT ( 'NONE',  ( 29.99999999999979750, 11.96639925780214320, 5.000000000000000000 ) ) ;
#3998=ORIENTED_EDGE ( 'NONE', *, *, #134154, .T. ) ;
#4000=ORIENTED_EDGE ( 'NONE', *, *, #123003, .T. ) ;
#4001=ORIENTED_EDGE ( 'NONE', *, *, #5014, .F. ) ;
#4002=VERTEX_POINT ( 'NONE', #76181 ) ;
#4003=ORIENTED_EDGE ( 'NONE', *, *, #128318, .T. ) ;
#4004=VECTOR ( 'NONE', #26767, 1000.000000000000000 ) ;
#4006=EDGE_CURVE ( 'NONE', #16006, #7225, #120343, .T. ) ;
#4007=CARTESIAN_POINT ( 'NONE',  ( -6.722509707016169678, 22.22500000000000142, 15.68697783646059918 ) ) ;
#4008=CARTESIAN_POINT ( 'NONE',  ( -50.99451991528749062, 28.92564299267973738, 4.000000000000000000 ) ) ;
#4009=EDGE_CURVE ( 'NONE', #42725, #118417, #131995, .T. ) ;
#4010=FACE_OUTER_BOUND ( 'NONE', #38579, .T. ) ;
#4012=LINE ( 'NONE', #67198, #7917 ) ;
#4015=FACE_OUTER_BOUND ( 'NONE', #87948, .T. ) ;
#4016=CARTESIAN_POINT ( 'NONE',  ( -7.362461875838964609, 22.22500000000000142, 4.000000000000000000 ) ) ;
#4017=VECTOR ( 'NONE', #106508, 1000.000000000000227 ) ;
#4018=CARTESIAN_POINT ( 'NONE',  ( -54.18398860626899705, 28.73617430169825226, 5.000000000000000000 ) ) ;
#4019=ORIENTED_EDGE ( 'NONE', *, *, #92997, .T. ) ;
#4020=ORIENTED_EDGE ( 'NONE', *, *, #299, .T. ) ;
#4021=VERTEX_POINT ( 'NONE', #118221 ) ;
#4022=DIRECTION ( 'NONE',  ( -0.000000000000000000, 0.000000000000000000, 1.000000000000000000 ) ) ;
#4023=LINE ( 'NONE', #16355, #125165 ) ;
#4024=ADVANCED_FACE ( 'NONE', ( #8031 ), #52271, .T. ) ;
#4025=CARTESIAN_POINT ( 'NONE',  ( 3.489213562373097322, -27.52281430457057709, 5.000000000000000000 ) ) ;
#4026=DIRECTION ( 'NONE',  ( -0.000000000000000000, 0.000000000000000000, 1.000000000000000000 ) ) ;
#4027=DIRECTION ( 'NONE',  ( 0.7071067811865486830, -0.7071067811865464625, -0.000000000000000000 ) ) ;
#4028=DIRECTION ( 'NONE',  ( -0.3543493200069162685, -0.000000000000000000, -0.9351131265310288487 ) ) ;
#4029=CARTESIAN_POINT ( 'NONE',  ( -10.21498419724184004, -3.740707523384238176, 15.76143240460121575 ) ) ;
#4030=CARTESIAN_POINT ( 'NONE',  ( 27.99507522778789692, -5.240707523384221744, 12.38332538355489731 ) ) ;
#4031=LINE ( 'NONE', #80957, #77330 ) ;
#4032=LINE ( 'NONE', #91133, #67550 ) ;
#4033=EDGE_CURVE ( 'NONE', #95860, #31073, #129838, .T. ) ;
#4034=ORIENTED_EDGE ( 'NONE', *, *, #67685, .T. ) ;
#4036=ORIENTED_EDGE ( 'NONE', *, *, #50050, .F. ) ;
#4037=VECTOR ( 'NONE', #138155, 999.9999999999998863 ) ;
#4038=LINE ( 'NONE', #57802, #4270 ) ;
#4039=LINE ( 'NONE', #100575, #92764 ) ;
#4040=VERTEX_POINT ( 'NONE', #52967 ) ;
#4041=VECTOR ( 'NONE', #92420, 1000.000000000000114 ) ;
#4042=LINE ( 'NONE', #94665, #62555 ) ;
#4043=DIRECTION ( 'NONE',  ( -0.000000000000000000, 0.3543493200069153248, 0.9351131265310292928 ) ) ;
#4044=ORIENTED_EDGE ( 'NONE', *, *, #138609, .F. ) ;
#4046=VERTEX_POINT ( 'NONE', #141430 ) ;
#4048=ORIENTED_EDGE ( 'NONE', *, *, #104810, .T. ) ;
#4049=VECTOR ( 'NONE', #94759, 1000.000000000000000 ) ;
#4051=FACE_OUTER_BOUND ( 'NONE', #35684, .T. ) ;
#4052=ADVANCED_FACE ( 'NONE', ( #42141 ), #86352, .F. ) ;
#4054=DIRECTION ( 'NONE',  ( -0.7071067811865486830, -0.7071067811865464625, 0.000000000000000000 ) ) ;
#4055=DIRECTION ( 'NONE',  ( -0.7071067811865487940, 0.7071067811865463515, -0.000000000000000000 ) ) ;
#4056=VERTEX_POINT ( 'NONE', #42852 ) ;
#4057=LINE ( 'NONE', #15662, #116322 ) ;
#4058=LINE ( 'NONE', #92533, #21797 ) ;
#4059=EDGE_CURVE ( 'NONE', #92120, #12987, #87050, .T. ) ;
#4060=LINE ( 'NONE', #38898, #103975 ) ;
#4062=CARTESIAN_POINT ( 'NONE',  ( 22.82816939922336985, -2.240707523384260824, 4.000000000000000000 ) ) ;
#4063=ORIENTED_EDGE ( 'NONE', *, *, #52192, .F. ) ;
#4065=ORIENTED_EDGE ( 'NONE', *, *, #38338, .F. ) ;
#4066=EDGE_CURVE ( 'NONE', #109845, #65462, #56615, .T. ) ;
#4068=CARTESIAN_POINT ( 'NONE',  ( -63.18398860626900415, 28.73617430169831621, 5.000000000000000000 ) ) ;
#4069=CARTESIAN_POINT ( 'NONE',  ( 10.17183060077640100, 12.75929247661558819, 4.000000000000000000 ) ) ;
#4070=DIRECTION ( 'NONE',  ( 0.7071067811865487940, 0.7071067811865463515, 0.000000000000000000 ) ) ;
#4071=CARTESIAN_POINT ( 'NONE',  ( -31.49999999999977973, 12.05218569542904383, 5.000000000000000000 ) ) ;
#4072=VERTEX_POINT ( 'NONE', #78322 ) ;
#4073=CARTESIAN_POINT ( 'NONE',  ( 2.282422613574298431, -21.73023691814492508, 5.000000000000000888 ) ) ;
#4075=VERTEX_POINT ( 'NONE', #23183 ) ;
#4076=CARTESIAN_POINT ( 'NONE',  ( 1.499999999999994449, 0.4311230773921780335, 4.000000000000000000 ) ) ;
#4077=EDGE_CURVE ( 'NONE', #115305, #86507, #101481, .T. ) ;
#4078=LINE ( 'NONE', #14301, #35635 ) ;
#4079=LINE ( 'NONE', #2701, #98374 ) ;
#4081=PLANE ( 'NONE',  #122392 ) ;
#4082=AXIS2_PLACEMENT_3D ( 'NONE', #42213, #88572, #102303 ) ;
#4083=CARTESIAN_POINT ( 'NONE',  ( 26.99999999999981526, -3.033600742197705369, 5.000000000000000000 ) ) ;
#4084=CARTESIAN_POINT ( 'NONE',  ( 21.48921356237309155, -27.52281430457070499, 5.000000000000000000 ) ) ;
#4085=CARTESIAN_POINT ( 'NONE',  ( -6.489213562373093325, -27.52281430457059841, 5.000000000000000000 ) ) ;
#4086=EDGE_LOOP ( 'NONE', ( #790, #100349, #114558, #107282 ) ) ;
#4087=VERTEX_POINT ( 'NONE', #91357 ) ;
#4088=ORIENTED_EDGE ( 'NONE', *, *, #61253, .F. ) ;
#4090=ORIENTED_EDGE ( 'NONE', *, *, #66742, .F. ) ;
#4091=CARTESIAN_POINT ( 'NONE',  ( 34.00193056682073944, -22.22500000000000142, 4.500000000000000888 ) ) ;
#4093=LINE ( 'NONE', #138972, #108189 ) ;
#4094=DIRECTION ( 'NONE',  ( 0.6830127018922181881, 0.6830127018922202975, -0.2588190451025214056 ) ) ;
#4096=CARTESIAN_POINT ( 'NONE',  ( 14.14114973822191423, 6.572112357556697759, 4.331981551378865092 ) ) ;
#4097=CARTESIAN_POINT ( 'NONE',  ( -54.18398860626899705, 28.73617430169825226, 5.000000000000000000 ) ) ;
#4099=ORIENTED_EDGE ( 'NONE', *, *, #119713, .T. ) ;
#4100=EDGE_CURVE ( 'NONE', #7339, #93773, #132732, .T. ) ;
#4102=CARTESIAN_POINT ( 'NONE',  ( 17.20710678118642178, -8.240707523384195099, 5.000000000000000000 ) ) ;
#4103=VERTEX_POINT ( 'NONE', #67471 ) ;
#4105=EDGE_CURVE ( 'NONE', #84436, #129923, #65432, .T. ) ;
#4106=DIRECTION ( 'NONE',  ( 1.000000000000000000, 0.000000000000000000, 0.000000000000000000 ) ) ;
#4107=ADVANCED_FACE ( 'NONE', ( #90635 ), #36248, .F. ) ;
#4108=DIRECTION ( 'NONE',  ( -0.7071067811865487940, 0.7071067811865463515, -0.000000000000000000 ) ) ;
#4109=PLANE ( 'NONE',  #36982 ) ;
#4110=CARTESIAN_POINT ( 'NONE',  ( 51.18398860626899705, 28.73617430169823095, 5.000000000000000000 ) ) ;
#4112=CARTESIAN_POINT ( 'NONE',  ( 3.291777089830458358, -15.74070752338412404, 19.73771281079098472 ) ) ;
#4113=LINE ( 'NONE', #6268, #136808 ) ;
#4114=ORIENTED_EDGE ( 'NONE', *, *, #63185, .F. ) ;
#4115=VECTOR ( 'NONE', #61154, 999.9999999999998863 ) ;
#4116=VERTEX_POINT ( 'NONE', #14483 ) ;
#4119=ADVANCED_FACE ( 'NONE', ( #11589 ), #134135, .F. ) ;
#4120=CARTESIAN_POINT ( 'NONE',  ( 66.29974487139159578, -27.71228299555252406, 4.000000000000000000 ) ) ;
#4121=ORIENTED_EDGE ( 'NONE', *, *, #134231, .T. ) ;
#4123=DIRECTION ( 'NONE',  ( -0.000000000000000000, -0.3543493200069152693, 0.9351131265310292928 ) ) ;
#4124=CARTESIAN_POINT ( 'NONE',  ( -34.49999999999976552, 18.05432934483075513, 4.994342998332167660 ) ) ;
#4125=VECTOR ( 'NONE', #42433, 999.9999999999998863 ) ;
#4126=DIRECTION ( 'NONE',  ( 0.6830127018922181881, 0.6830127018922202975, -0.2588190451025214056 ) ) ;
#4127=EDGE_LOOP ( 'NONE', ( #53914, #3819, #40808, #17412 ) ) ;
#4128=CARTESIAN_POINT ( 'NONE',  ( -16.95484226663322858, -21.74070752338405299, 21.72585301388580703 ) ) ;
#4130=VECTOR ( 'NONE', #122756, 1000.000000000000000 ) ;
#4131=ORIENTED_EDGE ( 'NONE', *, *, #26668, .F. ) ;
#4132=LINE ( 'NONE', #49874, #103733 ) ;
#4133=VERTEX_POINT ( 'NONE', #123273 ) ;
#4134=ORIENTED_EDGE ( 'NONE', *, *, #134870, .F. ) ;
#4135=DIRECTION ( 'NONE',  ( 0.7071067811865487940, 0.7071067811865463515, 0.000000000000000000 ) ) ;
#4136=VERTEX_POINT ( 'NONE', #58028 ) ;
#4139=AXIS2_PLACEMENT_3D ( 'NONE', #52002, #89435, #141888 ) ;
#4141=AXIS2_PLACEMENT_3D ( 'NONE', #55758, #44163, #88387 ) ;
#4142=DIRECTION ( 'NONE',  ( -2.781805975412905890E-17, 0.3543493200069152693, 0.9351131265310292928 ) ) ;
#4143=EDGE_CURVE ( 'NONE', #107270, #38431, #102229, .T. ) ;
#4144=FACE_OUTER_BOUND ( 'NONE', #102604, .T. ) ;
#4146=DIRECTION ( 'NONE',  ( 0.7071067811865487940, 0.7071067811865463515, 0.000000000000000000 ) ) ;
#4148=CARTESIAN_POINT ( 'NONE',  ( 17.99999999999986855, 9.631307414974335401, -9.079085613539497501 ) ) ;
#4149=LINE ( 'NONE', #79702, #139345 ) ;
#4150=DIRECTION ( 'NONE',  ( -0.3543493200069163240, 0.000000000000000000, 0.9351131265310288487 ) ) ;
#4151=CARTESIAN_POINT ( 'NONE',  ( -34.92500000000001137, 22.22500000000000142, 4.000000000000000000 ) ) ;
#4152=EDGE_CURVE ( 'NONE', #46538, #126680, #106441, .T. ) ;
#4153=ADVANCED_FACE ( 'NONE', ( #94164 ), #139130, .F. ) ;
#4154=DIRECTION ( 'NONE',  ( -0.000000000000000000, -0.3543493200069152693, 0.9351131265310292928 ) ) ;
#4155=ORIENTED_EDGE ( 'NONE', *, *, #21425, .T. ) ;
#4157=CARTESIAN_POINT ( 'NONE',  ( 2.816011393730999401, 28.73617430169785436, 5.000000000000000000 ) ) ;
#4158=ORIENTED_EDGE ( 'NONE', *, *, #4681, .F. ) ;
#4159=EDGE_LOOP ( 'NONE', ( #49526, #92374, #127745, #134673, #20295 ) ) ;
#4160=DIRECTION ( 'NONE',  ( 0.7071067811865487940, 0.7071067811865463515, -0.000000000000000000 ) ) ;
#4161=ORIENTED_EDGE ( 'NONE', *, *, #7495, .F. ) ;
#4162=VECTOR ( 'NONE', #37637, 1000.000000000000000 ) ;
#4163=FACE_OUTER_BOUND ( 'NONE', #52087, .T. ) ;
#4165=EDGE_CURVE ( 'NONE', #60444, #125103, #38380, .T. ) ;
#4166=CARTESIAN_POINT ( 'NONE',  ( 29.99451991528749417, 28.92564299267958816, 4.000000000000000000 ) ) ;
#4167=ADVANCED_FACE ( 'NONE', ( #93472 ), #15854, .F. ) ;
#4168=CARTESIAN_POINT ( 'NONE',  ( -48.18398860626899705, 28.73617430169820608, 5.000000000000000000 ) ) ;
#4169=EDGE_LOOP ( 'NONE', ( #88080, #119651, #87715, #129237 ) ) ;
#4170=DIRECTION ( 'NONE',  ( -0.7071067811865486830, -0.7071067811865464625, -0.000000000000000000 ) ) ;
#4171=ORIENTED_EDGE ( 'NONE', *, *, #40357, .T. ) ;
#4172=DIRECTION ( 'NONE',  ( -0.000000000000000000, -0.3543493200069152693, 0.9351131265310292928 ) ) ;
#4173=ADVANCED_FACE ( 'NONE', ( #70343 ), #114489, .F. ) ;
#4175=ADVANCED_FACE ( 'NONE', ( #4243 ), #81924, .T. ) ;
#4176=DIRECTION ( 'NONE',  ( 0.7071067811865486830, -0.7071067811865464625, -0.000000000000000000 ) ) ;
#4177=PLANE ( 'NONE',  #65164 ) ;
#4178=ORIENTED_EDGE ( 'NONE', *, *, #54914, .T. ) ;
#4180=ORIENTED_EDGE ( 'NONE', *, *, #39223, .F. ) ;
#4181=CARTESIAN_POINT ( 'NONE',  ( -26.20710678118635428, 3.759292476615680112, 5.000000000000000000 ) ) ;
#4183=EDGE_CURVE ( 'NONE', #81752, #61225, #5714, .T. ) ;
#4184=DIRECTION ( 'NONE',  ( -0.7071067811865486830, -0.7071067811865464625, 0.000000000000000000 ) ) ;
#4185=VECTOR ( 'NONE', #52864, 1000.000000000000000 ) ;
#4187=VERTEX_POINT ( 'NONE', #96041 ) ;
#4188=LINE ( 'NONE', #36194, #37008 ) ;
#4189=VECTOR ( 'NONE', #4740, 1000.000000000000000 ) ;
#4190=CARTESIAN_POINT ( 'NONE',  ( -3.469446951953614189E-15, -1.068876922607807645, 4.000000000000000000 ) ) ;
#4191=CARTESIAN_POINT ( 'NONE',  ( -3.489213562373097322, -27.52281430457057709, 5.000000000000000000 ) ) ;
#4194=EDGE_CURVE ( 'NONE', #105497, #47322, #128685, .T. ) ;
#4195=FACE_OUTER_BOUND ( 'NONE', #93538, .T. ) ;
#4198=ORIENTED_EDGE ( 'NONE', *, *, #110254, .F. ) ;
#4199=VERTEX_POINT ( 'NONE', #49729 ) ;
#4200=CARTESIAN_POINT ( 'NONE',  ( 36.18398860626899705, 28.73617430169812437, 5.000000000000000000 ) ) ;
#4201=ADVANCED_FACE ( 'NONE', ( #19904 ), #38827, .F. ) ;
#4202=CARTESIAN_POINT ( 'NONE',  ( -28.77325839282149289, -11.24070752338416845, 18.24660765846975963 ) ) ;
#4203=CARTESIAN_POINT ( 'NONE',  ( -45.48921356237309510, -27.52281430457087197, 5.000000000000000000 ) ) ;
#4205=ORIENTED_EDGE ( 'NONE', *, *, #123667, .T. ) ;
#4206=CARTESIAN_POINT ( 'NONE',  ( 7.499999999999951150, -10.04351517176477948, -1.623559851933805698 ) ) ;
#4208=ORIENTED_EDGE ( 'NONE', *, *, #83296, .F. ) ;
#4209=DIRECTION ( 'NONE',  ( 0.7071067811865486830, -0.7071067811865464625, -0.000000000000000000 ) ) ;
#4210=CARTESIAN_POINT ( 'NONE',  ( 6.668467411598530070, -18.74070752338408496, 20.73178291233842430 ) ) ;
#4211=ADVANCED_FACE ( 'NONE', ( #19209 ), #72212, .T. ) ;
#4213=CARTESIAN_POINT ( 'NONE',  ( -24.69326993309583429, -3.740707523384241728, 12.88036043432873257 ) ) ;
#4221=PLANE ( 'NONE',  #97560 ) ;
#4222=PLANE ( 'NONE',  #33850 ) ;
#4223=EDGE_LOOP ( 'NONE', ( #99920, #142610, #110916, #116699 ) ) ;
#4224=ORIENTED_EDGE ( 'NONE', *, *, #5775, .T. ) ;
#4227=ORIENTED_EDGE ( 'NONE', *, *, #131620, .F. ) ;
#4229=CARTESIAN_POINT ( 'NONE',  ( -27.18398860626900060, 28.73617430169806042, 5.000000000000000000 ) ) ;
#4231=ORIENTED_EDGE ( 'NONE', *, *, #106630, .T. ) ;
#4234=VECTOR ( 'NONE', #60382, 1000.000000000000000 ) ;
#4235=DIRECTION ( 'NONE',  ( -0.7071067811865486830, -0.7071067811865464625, -0.000000000000000000 ) ) ;
#4236=LINE ( 'NONE', #59443, #108950 ) ;
#4238=DIRECTION ( 'NONE',  ( -0.3543493200069162685, -0.000000000000000000, -0.9351131265310288487 ) ) ;
#4240=AXIS2_PLACEMENT_3D ( 'NONE', #95538, #83253, #29563 ) ;
#4241=PLANE ( 'NONE',  #97905 ) ;
#4242=CARTESIAN_POINT ( 'NONE',  ( 45.48921356237309510, -27.52281430457087197, 5.000000000000000000 ) ) ;
#4243=FACE_OUTER_BOUND ( 'NONE', #51956, .T. ) ;
#4244=VECTOR ( 'NONE', #24717, 999.9999999999998863 ) ;
#4245=CARTESIAN_POINT ( 'NONE',  ( 16.31507112947232230, 22.22500000000000142, -14.41677840540084254 ) ) ;
#4246=DIRECTION ( 'NONE',  ( 0.7071067811865486830, -0.7071067811865464625, -0.000000000000000000 ) ) ;
#4247=DIRECTION ( 'NONE',  ( 0.6830127018922181881, 0.6830127018922202975, -0.2588190451025214056 ) ) ;
#4248=VECTOR ( 'NONE', #124314, 1000.000000000000227 ) ;
#4249=CARTESIAN_POINT ( 'NONE',  ( 13.17183060077637613, -11.24070752338416668, 4.000000000000000000 ) ) ;
#4250=LINE ( 'NONE', #69616, #100066 ) ;
#4251=EDGE_LOOP ( 'NONE', ( #13017, #99300, #14901, #42051 ) ) ;
#4252=VERTEX_POINT ( 'NONE', #127241 ) ;
#4254=ORIENTED_EDGE ( 'NONE', *, *, #4566, .F. ) ;
#4255=ADVANCED_FACE ( 'NONE', ( #129382 ), #30069, .F. ) ;
#4256=CARTESIAN_POINT ( 'NONE',  ( 13.82816939922343558, 18.75929247661552424, 4.000000000000000000 ) ) ;
#4258=LINE ( 'NONE', #68216, #122068 ) ;
#4259=EDGE_LOOP ( 'NONE', ( #71090, #59683, #72791, #79294 ) ) ;
#4261=FACE_OUTER_BOUND ( 'NONE', #136404, .T. ) ;
#4262=VECTOR ( 'NONE', #133760, 1000.000000000000000 ) ;
#4264=ORIENTED_EDGE ( 'NONE', *, *, #82601, .T. ) ;
#4268=LINE ( 'NONE', #104347, #40868 ) ;
#4269=VECTOR ( 'NONE', #47698, 1000.000000000000227 ) ;
#4270=VECTOR ( 'NONE', #92517, 1000.000000000000114 ) ;
#4271=EDGE_LOOP ( 'NONE', ( #81073, #94967, #15577, #132278 ) ) ;
#4272=ORIENTED_EDGE ( 'NONE', *, *, #35365, .F. ) ;
#4274=ORIENTED_EDGE ( 'NONE', *, *, #20642, .F. ) ;
#4275=DIRECTION ( 'NONE',  ( -0.7071067811865487940, 0.7071067811865463515, 0.000000000000000000 ) ) ;
#4276=EDGE_CURVE ( 'NONE', #37184, #105472, #130125, .T. ) ;
#4279=VERTEX_POINT ( 'NONE', #39557 ) ;
#4281=ORIENTED_EDGE ( 'NONE', *, *, #121146, .F. ) ;
#4282=LINE ( 'NONE', #115215, #10809 ) ;
#4284=ORIENTED_EDGE ( 'NONE', *, *, #142424, .F. ) ;
#4286=CARTESIAN_POINT ( 'NONE',  ( -27.79333936457828358, 21.75929247661549581, 4.998822639870701856 ) ) ;
#4287=EDGE_CURVE ( 'NONE', #10814, #4770, #6145, .T. ) ;
#4288=PLANE ( 'NONE',  #65190 ) ;
#4289=ORIENTED_EDGE ( 'NONE', *, *, #77343, .F. ) ;
#4290=LINE ( 'NONE', #28271, #101564 ) ;
#4291=CARTESIAN_POINT ( 'NONE',  ( -14.51078643762690490, -27.52281430457045275, 5.000000000000000000 ) ) ;
#4292=EDGE_CURVE ( 'NONE', #105516, #33114, #116381, .T. ) ;
#4293=DIRECTION ( 'NONE',  ( -0.6830127018922181881, 0.6830127018922202975, -0.2588190451025214056 ) ) ;
#4294=CARTESIAN_POINT ( 'NONE',  ( 11.01088028653940754, -22.02621442084248571, 4.990779571109220214 ) ) ;
#4295=FACE_BOUND ( 'NONE', #134171, .T. ) ;
#4296=ORIENTED_EDGE ( 'NONE', *, *, #117997, .T. ) ;
#4297=LINE ( 'NONE', #92801, #36480 ) ;
#4298=DIRECTION ( 'NONE',  ( -0.7071067811865486830, -0.7071067811865464625, 0.000000000000000000 ) ) ;
#4301=CARTESIAN_POINT ( 'NONE',  ( 30.29974487139158867, -27.71228299555227537, 4.000000000000000000 ) ) ;
#4302=VERTEX_POINT ( 'NONE', #50423 ) ;
#4303=ADVANCED_FACE ( 'NONE', ( #94608 ), #138863, .T. ) ;
#4305=ORIENTED_EDGE ( 'NONE', *, *, #12597, .F. ) ;
#4307=ORIENTED_EDGE ( 'NONE', *, *, #110008, .F. ) ;
#4308=CARTESIAN_POINT ( 'NONE',  ( 35.99451991528749772, 28.92564299267963079, 4.000000000000000000 ) ) ;
#4309=CARTESIAN_POINT ( 'NONE',  ( 15.18398860626900237, 28.73617430169797871, 5.000000000000000000 ) ) ;
#4310=CARTESIAN_POINT ( 'NONE',  ( -21.18398860626899349, 28.73617430169802134, 5.000000000000000000 ) ) ;
#4311=EDGE_CURVE ( 'NONE', #79253, #5780, #8294, .T. ) ;
#4312=ORIENTED_EDGE ( 'NONE', *, *, #76951, .F. ) ;
#4313=DIRECTION ( 'NONE',  ( 0.7071067811865486830, -0.7071067811865464625, -0.000000000000000000 ) ) ;
#4314=CARTESIAN_POINT ( 'NONE',  ( 69.18398860626899705, 28.73617430169835529, 5.000000000000000000 ) ) ;
#4315=EDGE_CURVE ( 'NONE', #103174, #5826, #70929, .T. ) ;
#4316=EDGE_CURVE ( 'NONE', #133459, #99209, #139598, .T. ) ;
#4319=DIRECTION ( 'NONE',  ( 0.6830127018922180770, -0.6830127018922204085, -0.2588190451025213501 ) ) ;
#4320=LINE ( 'NONE', #48624, #50576 ) ;
#4321=PLANE ( 'NONE',  #79570 ) ;
#4322=ORIENTED_EDGE ( 'NONE', *, *, #67245, .F. ) ;
#4323=VERTEX_POINT ( 'NONE', #30825 ) ;
#4325=VERTEX_POINT ( 'NONE', #52544 ) ;
#4326=ORIENTED_EDGE ( 'NONE', *, *, #125652, .T. ) ;
#4328=VECTOR ( 'NONE', #107666, 1000.000000000000227 ) ;
#4329=ORIENTED_EDGE ( 'NONE', *, *, #33893, .F. ) ;
#4330=EDGE_CURVE ( 'NONE', #81604, #92832, #75051, .T. ) ;
#4332=ORIENTED_EDGE ( 'NONE', *, *, #14074, .F. ) ;
#4333=LINE ( 'NONE', #36335, #42126 ) ;
#4334=FACE_OUTER_BOUND ( 'NONE', #92913, .T. ) ;
#4335=ADVANCED_FACE ( 'NONE', ( #89458 ), #22737, .F. ) ;
#4336=ADVANCED_FACE ( 'NONE', ( #9744 ), #110473, .F. ) ;
#4337=DIRECTION ( 'NONE',  ( -0.6830127018922180770, -0.6830127018922204085, -0.2588190451025213501 ) ) ;
#4338=EDGE_LOOP ( 'NONE', ( #53119, #113201, #137774, #82378 ) ) ;
#4340=VECTOR ( 'NONE', #113927, 1000.000000000000000 ) ;
#4341=EDGE_LOOP ( 'NONE', ( #115221, #1741, #89023, #22914 ) ) ;
#4342=FACE_OUTER_BOUND ( 'NONE', #123688, .T. ) ;
#4343=CARTESIAN_POINT ( 'NONE',  ( 15.48921356237309510, -27.52281430457066236, 5.000000000000000000 ) ) ;
#4345=EDGE_LOOP ( 'NONE', ( #112899, #19970, #51704, #46723 ) ) ;
#4348=ADVANCED_FACE ( 'NONE', ( #77881 ), #44576, .F. ) ;
#4349=CARTESIAN_POINT ( 'NONE',  ( -8.999999999999944933, -2.904428200921325143, -6.989807076074924019 ) ) ;
#4350=DIRECTION ( 'NONE',  ( -0.7071067811865486830, 0.7071067811865464625, 0.000000000000000000 ) ) ;
#4351=EDGE_LOOP ( 'NONE', ( #103833, #86726, #24032, #24093, #31848, #24286 ) ) ;
#4352=ORIENTED_EDGE ( 'NONE', *, *, #81520, .F. ) ;
#4353=EDGE_LOOP ( 'NONE', ( #81695, #43172, #9424, #135312 ) ) ;
#4354=AXIS2_PLACEMENT_3D ( 'NONE', #111621, #70303, #47824 ) ;
#4356=CARTESIAN_POINT ( 'NONE',  ( 39.18398860626899705, 28.73617430169814568, 5.000000000000000000 ) ) ;
#4358=EDGE_CURVE ( 'NONE', #94978, #13138, #1002, .T. ) ;
#4359=FACE_OUTER_BOUND ( 'NONE', #98391, .T. ) ;
#4361=EDGE_LOOP ( 'NONE', ( #93428, #89119, #88624, #38765 ) ) ;
#4362=FACE_OUTER_BOUND ( 'NONE', #126626, .T. ) ;
#4363=LINE ( 'NONE', #80593, #4752 ) ;
#4364=DIRECTION ( 'NONE',  ( -0.000000000000000000, 0.000000000000000000, 1.000000000000000000 ) ) ;
#4365=ORIENTED_EDGE ( 'NONE', *, *, #81342, .T. ) ;
#4366=PLANE ( 'NONE',  #102174 ) ;
#4367=VECTOR ( 'NONE', #82975, 1000.000000000000000 ) ;
#4368=CARTESIAN_POINT ( 'NONE',  ( 24.48921356237309510, -27.52281430457072631, 5.000000000000000000 ) ) ;
#4370=ORIENTED_EDGE ( 'NONE', *, *, #109635, .F. ) ;
#4371=CARTESIAN_POINT ( 'NONE',  ( 2.999999999999988898, 20.96639925780204905, 5.000000000000000000 ) ) ;
#4373=ORIENTED_EDGE ( 'NONE', *, *, #77923, .F. ) ;
#4375=VECTOR ( 'NONE', #37484, 1000.000000000000000 ) ;
#4376=CARTESIAN_POINT ( 'NONE',  ( -11.29289321881337749, 8.259292476615629042, 5.000000000000000000 ) ) ;
#4377=VERTEX_POINT ( 'NONE', #54713 ) ;
#4379=VECTOR ( 'NONE', #105491, 999.9999999999998863 ) ;
#4380=EDGE_CURVE ( 'NONE', #78474, #15318, #277, .T. ) ;
#4381=ADVANCED_FACE ( 'NONE', ( #45283 ), #120636, .F. ) ;
#4382=FACE_OUTER_BOUND ( 'NONE', #91867, .T. ) ;
#4383=ORIENTED_EDGE ( 'NONE', *, *, #142724, .F. ) ;
#4384=CARTESIAN_POINT ( 'NONE',  ( 28.49999999999979750, 10.08746187583915344, 4.000000000000000000 ) ) ;
#4387=CARTESIAN_POINT ( 'NONE',  ( 13.49999999999991296, -1.533600742197722910, 5.000000000000000000 ) ) ;
#4388=VECTOR ( 'NONE', #20467, 999.9999999999998863 ) ;
#4389=CARTESIAN_POINT ( 'NONE',  ( -24.48921356237309510, -27.52281430457072631, 5.000000000000000000 ) ) ;
#4392=CARTESIAN_POINT ( 'NONE',  ( -11.99999999999991651, -4.447814304570786526, 5.000000000000000000 ) ) ;
#4394=EDGE_LOOP ( 'NONE', ( #43317, #106850, #131338, #104280 ) ) ;
#4398=ORIENTED_EDGE ( 'NONE', *, *, #27406, .F. ) ;
#4399=ORIENTED_EDGE ( 'NONE', *, *, #63527, .F. ) ;
#4400=EDGE_LOOP ( 'NONE', ( #131207, #15353, #116582, #68784 ) ) ;
#4401=DIRECTION ( 'NONE',  ( -0.6830127018922180770, -0.6830127018922204085, -0.2588190451025213501 ) ) ;
#4402=DIRECTION ( 'NONE',  ( 0.7071067811865486830, -0.7071067811865464625, -0.000000000000000000 ) ) ;
#4403=ORIENTED_EDGE ( 'NONE', *, *, #118266, .F. ) ;
#4404=CARTESIAN_POINT ( 'NONE',  ( -30.32816939922331656, 14.25929247661556865, 4.000000000000000000 ) ) ;
#4405=LINE ( 'NONE', #35729, #32519 ) ;
#4406=LINE ( 'NONE', #28390, #81187 ) ;
#4408=ORIENTED_EDGE ( 'NONE', *, *, #102549, .T. ) ;
#4409=CARTESIAN_POINT ( 'NONE',  ( -14.99451991528749595, 28.92564299267948513, 4.000000000000000000 ) ) ;
#4410=DIRECTION ( 'NONE',  ( -0.6830127018922181881, 0.6830127018922202975, -0.2588190451025214056 ) ) ;
#4411=CARTESIAN_POINT ( 'NONE',  ( 34.49999999999976552, 4.464255608400454101, 4.994342998332159667 ) ) ;
#4412=CARTESIAN_POINT ( 'NONE',  ( 11.81601139373100651, 28.73617430169779041, 5.000000000000000000 ) ) ;
#4413=PLANE ( 'NONE',  #125573 ) ;
#4414=LINE ( 'NONE', #46630, #119858 ) ;
#4416=CARTESIAN_POINT ( 'NONE',  ( 11.99999999999991473, 7.931123077392106424, 4.000000000000000000 ) ) ;
#4417=DIRECTION ( 'NONE',  ( -0.6830127018922181881, 0.6830127018922202975, -0.2588190451025214056 ) ) ;
#4418=VERTEX_POINT ( 'NONE', #88039 ) ;
#4419=ORIENTED_EDGE ( 'NONE', *, *, #66726, .T. ) ;
#4421=EDGE_LOOP ( 'NONE', ( #134278, #139734, #52048, #87188, #21958 ) ) ;
#4423=DIRECTION ( 'NONE',  ( -0.6830127018922180770, -0.6830127018922204085, -0.2588190451025213501 ) ) ;
#4425=CARTESIAN_POINT ( 'NONE',  ( 24.29974487139158867, -27.71228299555223273, 4.000000000000000000 ) ) ;
#4427=ORIENTED_EDGE ( 'NONE', *, *, #139798, .T. ) ;
#4428=DIRECTION ( 'NONE',  ( 1.000000000000000000, 0.000000000000000000, 0.000000000000000000 ) ) ;
#4429=DIRECTION ( 'NONE',  ( -0.7071067811865486830, -0.7071067811865464625, 0.000000000000000000 ) ) ;
#4430=CARTESIAN_POINT ( 'NONE',  ( -45.29974487139158867, -27.71228299555237840, 4.000000000000000000 ) ) ;
#4432=ORIENTED_EDGE ( 'NONE', *, *, #85426, .F. ) ;
#4433=PLANE ( 'NONE',  #68834 ) ;
#4434=VERTEX_POINT ( 'NONE', #32977 ) ;
#4435=LINE ( 'NONE', #57494, #68115 ) ;
#4436=VECTOR ( 'NONE', #13293, 999.9999999999998863 ) ;
#4437=VECTOR ( 'NONE', #54218, 1000.000000000000000 ) ;
#4438=AXIS2_PLACEMENT_3D ( 'NONE', #31109, #140553, #97014 ) ;
#4439=CARTESIAN_POINT ( 'NONE',  ( -2.903329358125931403, -2.240707523384260824, 15.26439735382751905 ) ) ;
#4440=DIRECTION ( 'NONE',  ( 0.7071067811865487940, -0.7071067811865463515, 0.000000000000000000 ) ) ;
#4441=VECTOR ( 'NONE', #45431, 1000.000000000000000 ) ;
#4442=ADVANCED_FACE ( 'NONE', ( #8986 ), #66302, .T. ) ;
#4443=DIRECTION ( 'NONE',  ( -0.000000000000000000, 0.000000000000000000, 1.000000000000000000 ) ) ;
#4444=EDGE_LOOP ( 'NONE', ( #28106, #142001, #131924, #126948 ) ) ;
#4447=VERTEX_POINT ( 'NONE', #22045 ) ;
#4448=DIRECTION ( 'NONE',  ( 0.7071067811865487940, 0.7071067811865463515, 0.000000000000000000 ) ) ;
#4449=CARTESIAN_POINT ( 'NONE',  ( 34.92499999999998295, 21.73644205237997795, 4.195230610814717487 ) ) ;
#4450=DIRECTION ( 'NONE',  ( 0.7071067811865487940, 0.7071067811865463515, 0.000000000000000000 ) ) ;
#4451=EDGE_CURVE ( 'NONE', #71937, #106339, #24218, .T. ) ;
#4452=EDGE_CURVE ( 'NONE', #84436, #44653, #69896, .T. ) ;
#4453=VECTOR ( 'NONE', #74162, 1000.000000000000000 ) ;
#4455=ORIENTED_EDGE ( 'NONE', *, *, #127119, .F. ) ;
#4456=CARTESIAN_POINT ( 'NONE',  ( -32.99999999999976552, 12.83542986846994083, -1.025386466790294548 ) ) ;
#4457=EDGE_CURVE ( 'NONE', #52896, #18442, #113336, .T. ) ;
#4458=FACE_OUTER_BOUND ( 'NONE', #59021, .T. ) ;
#4460=ORIENTED_EDGE ( 'NONE', *, *, #39893, .T. ) ;
#4461=VECTOR ( 'NONE', #55652, 1000.000000000000000 ) ;
#4463=DIRECTION ( 'NONE',  ( -0.000000000000000000, 0.3543493200069153248, 0.9351131265310291818 ) ) ;
#4464=EDGE_LOOP ( 'NONE', ( #21588, #64579, #72111, #86706 ) ) ;
#4465=ADVANCED_FACE ( 'NONE', ( #103875 ), #58322, .F. ) ;
#4467=PLANE ( 'NONE',  #118231 ) ;
#4468=ORIENTED_EDGE ( 'NONE', *, *, #2997, .T. ) ;
#4469=CARTESIAN_POINT ( 'NONE',  ( 0.000000000000000000, 0.000000000000000000, 5.000000000000000000 ) ) ;
#4470=AXIS2_PLACEMENT_3D ( 'NONE', #57500, #90092, #13231 ) ;
#4471=EDGE_CURVE ( 'NONE', #134440, #113476, #91606, .T. ) ;
#4473=DIRECTION ( 'NONE',  ( 0.7071067811865486830, -0.7071067811865464625, -0.000000000000000000 ) ) ;
#4474=AXIS2_PLACEMENT_3D ( 'NONE', #130539, #10847, #42820 ) ;
#4475=FACE_BOUND ( 'NONE', #80602, .T. ) ;
#4476=DIRECTION ( 'NONE',  ( 0.7071067811865487940, -0.7071067811865463515, -0.000000000000000000 ) ) ;
#4477=FACE_OUTER_BOUND ( 'NONE', #86662, .T. ) ;
#4478=CARTESIAN_POINT ( 'NONE',  ( -2.816011393730999401, 28.73617430169785436, 5.000000000000000000 ) ) ;
#4479=VECTOR ( 'NONE', #39451, 1000.000000000000227 ) ;
#4480=LINE ( 'NONE', #115409, #80506 ) ;
#4481=CARTESIAN_POINT ( 'NONE',  ( -36.18398860626899705, 28.73617430169812437, 5.000000000000000000 ) ) ;
#4483=VECTOR ( 'NONE', #73510, 1000.000000000000000 ) ;
#4484=ADVANCED_FACE ( 'NONE', ( #68464 ), #15428, .T. ) ;
#4485=PLANE ( 'NONE',  #111939 ) ;
#4486=EDGE_LOOP ( 'NONE', ( #96374, #22334, #37714, #16444 ) ) ;
#4487=ORIENTED_EDGE ( 'NONE', *, *, #70818, .T. ) ;
#4489=ORIENTED_EDGE ( 'NONE', *, *, #128918, .F. ) ;
#4490=DIRECTION ( 'NONE',  ( -0.3543493200069162685, -0.000000000000000000, -0.9351131265310288487 ) ) ;
#4491=CARTESIAN_POINT ( 'NONE',  ( 17.99999999999987921, -10.44781430457071814, 5.000000000000000000 ) ) ;
#4492=EDGE_CURVE ( 'NONE', #14551, #118295, #47444, .T. ) ;
#4494=FACE_OUTER_BOUND ( 'NONE', #58383, .T. ) ;
#4496=ADVANCED_FACE ( 'NONE', ( #124233 ), #37957, .F. ) ;
#4497=CARTESIAN_POINT ( 'NONE',  ( -54.18398860626899705, 28.73617430169825226, 5.000000000000000000 ) ) ;
#4498=DIRECTION ( 'NONE',  ( -0.7071067811865486830, -0.7071067811865464625, 0.000000000000000000 ) ) ;
#4499=EDGE_CURVE ( 'NONE', #49517, #138986, #48115, .T. ) ;
#4501=DIRECTION ( 'NONE',  ( 0.7071067811865486830, -0.7071067811865464625, -0.000000000000000000 ) ) ;
#4504=ORIENTED_EDGE ( 'NONE', *, *, #54253, .F. ) ;
#4505=DIRECTION ( 'NONE',  ( 0.7071067811865487940, 0.7071067811865463515, -0.000000000000000000 ) ) ;
#4506=LINE ( 'NONE', #37943, #136957 ) ;
#4507=ORIENTED_EDGE ( 'NONE', *, *, #108622, .T. ) ;
#4508=EDGE_CURVE ( 'NONE', #26708, #125846, #3829, .T. ) ;
#4509=ORIENTED_EDGE ( 'NONE', *, *, #129381, .F. ) ;
#4510=ORIENTED_EDGE ( 'NONE', *, *, #58996, .F. ) ;
#4511=FACE_OUTER_BOUND ( 'NONE', #19918, .T. ) ;
#4512=CARTESIAN_POINT ( 'NONE',  ( 23.99451991528749062, 28.92564299267954908, 4.000000000000000000 ) ) ;
#4513=ORIENTED_EDGE ( 'NONE', *, *, #58773, .T. ) ;
#4514=DIRECTION ( 'NONE',  ( -0.000000000000000000, 0.000000000000000000, 1.000000000000000000 ) ) ;
#4515=CARTESIAN_POINT ( 'NONE',  ( -3.299744871391591339, -27.71228299555208352, 4.000000000000000000 ) ) ;
#4518=ORIENTED_EDGE ( 'NONE', *, *, #126994, .F. ) ;
#4519=EDGE_CURVE ( 'NONE', #110495, #113106, #26356, .T. ) ;
#4520=LINE ( 'NONE', #56880, #57366 ) ;
#4521=LINE ( 'NONE', #35111, #120700 ) ;
#4522=DIRECTION ( 'NONE',  ( 1.000000000000000000, 0.000000000000000000, 0.000000000000000000 ) ) ;
#4523=CARTESIAN_POINT ( 'NONE',  ( -35.56319896779149303, -12.74070752338414891, 9.898150129686460019 ) ) ;
#4524=VERTEX_POINT ( 'NONE', #126363 ) ;
#4525=CARTESIAN_POINT ( 'NONE',  ( -34.92500000000001137, 22.22500000000000142, 4.000000000000000000 ) ) ;
#4528=EDGE_CURVE ( 'NONE', #134155, #12475, #123555, .T. ) ;
#4529=DIRECTION ( 'NONE',  ( -0.7071067811865487940, 0.7071067811865463515, -0.000000000000000000 ) ) ;
#4531=ORIENTED_EDGE ( 'NONE', *, *, #67079, .T. ) ;
#4532=CARTESIAN_POINT ( 'NONE',  ( -33.43654659701051912, -22.22500000000000142, 5.564030635702776451 ) ) ;
#4533=EDGE_CURVE ( 'NONE', #48333, #79691, #124938, .T. ) ;
#4535=DIRECTION ( 'NONE',  ( -0.7071067811865486830, -0.7071067811865464625, -0.000000000000000000 ) ) ;
#4536=DIRECTION ( 'NONE',  ( 1.000000000000000000, 0.000000000000000000, 0.000000000000000000 ) ) ;
#4539=VECTOR ( 'NONE', #114583, 1000.000000000000000 ) ;
#4541=AXIS2_PLACEMENT_3D ( 'NONE', #86986, #63826, #53660 ) ;
#4542=CARTESIAN_POINT ( 'NONE',  ( -14.81601139373099585, 28.73617430169776910, 5.000000000000000000 ) ) ;
#4543=CARTESIAN_POINT ( 'NONE',  ( 34.42499999999998295, -22.22500000000000142, 0.4999999999999995559 ) ) ;
#4544=DIRECTION ( 'NONE',  ( -0.000000000000000000, -0.3543493200069153248, -0.9351131265310291818 ) ) ;
#4545=AXIS2_PLACEMENT_3D ( 'NONE', #77860, #122049, #125657 ) ;
#4546=CARTESIAN_POINT ( 'NONE',  ( -22.49999999999984368, -1.695981523266240076, 4.571483868317929300 ) ) ;
#4547=EDGE_CURVE ( 'NONE', #64350, #141614, #4520, .T. ) ;
#4549=ORIENTED_EDGE ( 'NONE', *, *, #137433, .T. ) ;
#4550=ORIENTED_EDGE ( 'NONE', *, *, #31669, .T. ) ;
#4551=FACE_OUTER_BOUND ( 'NONE', #31005, .T. ) ;
#4552=VECTOR ( 'NONE', #63538, 1000.000000000000000 ) ;
#4553=PLANE ( 'NONE',  #89903 ) ;
#4555=DIRECTION ( 'NONE',  ( -0.3543493200069162685, -0.000000000000000000, -0.9351131265310288487 ) ) ;
#4556=ADVANCED_FACE ( 'NONE', ( #93030 ), #137262, .F. ) ;
#4557=CARTESIAN_POINT ( 'NONE',  ( 34.92499999999998295, 6.324594729295675677, 11.02525794543158000 ) ) ;
#4558=LINE ( 'NONE', #123593, #106114 ) ;
#4559=LINE ( 'NONE', #37265, #106922 ) ;
#4560=ORIENTED_EDGE ( 'NONE', *, *, #134300, .T. ) ;
#4561=CARTESIAN_POINT ( 'NONE',  ( -2.510786437626908008, -27.52281430457053446, 5.000000000000000000 ) ) ;
#4562=CARTESIAN_POINT ( 'NONE',  ( -0.7933393645784717618, 21.75929247661549581, 4.998822639870701856 ) ) ;
#4563=AXIS2_PLACEMENT_3D ( 'NONE', #130558, #41377, #43531 ) ;
#4564=DIRECTION ( 'NONE',  ( -0.6830127018922181881, 0.6830127018922202975, -0.2588190451025214056 ) ) ;
#4566=EDGE_CURVE ( 'NONE', #58909, #131858, #101038, .T. ) ;
#4567=DIRECTION ( 'NONE',  ( -0.7071067811865486830, 0.7071067811865464625, 0.000000000000000000 ) ) ;
#4569=EDGE_CURVE ( 'NONE', #136335, #119204, #24909, .T. ) ;
#4570=ORIENTED_EDGE ( 'NONE', *, *, #75403, .T. ) ;
#4572=ORIENTED_EDGE ( 'NONE', *, *, #10276, .F. ) ;
#4573=ORIENTED_EDGE ( 'NONE', *, *, #89697, .F. ) ;
#4574=CARTESIAN_POINT ( 'NONE',  ( -16.49999999999988631, 19.39370406404965763, 1.459788787078239558 ) ) ;
#4575=VECTOR ( 'NONE', #55135, 1000.000000000000000 ) ;
#4576=LINE ( 'NONE', #69957, #62312 ) ;
#4578=FACE_OUTER_BOUND ( 'NONE', #91247, .T. ) ;
#4579=ADVANCED_FACE ( 'NONE', ( #13303 ), #57576, .F. ) ;
#4580=PLANE ( 'NONE',  #139132 ) ;
#4583=VERTEX_POINT ( 'NONE', #60437 ) ;
#4584=CARTESIAN_POINT ( 'NONE',  ( -34.49999999999974420, -17.94567065516885762, 4.994342998332165884 ) ) ;
#4585=CARTESIAN_POINT ( 'NONE',  ( -13.26601651615776767, 1.700382741644379081, 5.000000000000000000 ) ) ;
#4586=VECTOR ( 'NONE', #105241, 1000.000000000000000 ) ;
#4587=CARTESIAN_POINT ( 'NONE',  ( 1.499999999999990896, 13.08746187583910725, 4.000000000000000000 ) ) ;
#4591=VECTOR ( 'NONE', #5242, 1000.000000000000227 ) ;
#4592=ORIENTED_EDGE ( 'NONE', *, *, #58124, .T. ) ;
#4593=VERTEX_POINT ( 'NONE', #71300 ) ;
#4595=DIRECTION ( 'NONE',  ( 0.3543493200069162685, -0.000000000000000000, -0.9351131265310288487 ) ) ;
#4596=LINE ( 'NONE', #61248, #25435 ) ;
#4598=AXIS2_PLACEMENT_3D ( 'NONE', #51576, #19636, #16780 ) ;
#4599=ORIENTED_EDGE ( 'NONE', *, *, #42924, .T. ) ;
#4600=CARTESIAN_POINT ( 'NONE',  ( -2.999999999999975575, -21.03360074219752107, 5.000000000000000000 ) ) ;
#4601=DIRECTION ( 'NONE',  ( -0.3543493200069162685, -0.000000000000000000, -0.9351131265310288487 ) ) ;
#4603=DIRECTION ( 'NONE',  ( -0.7071067811865486830, 0.7071067811865464625, 0.000000000000000000 ) ) ;
#4604=ORIENTED_EDGE ( 'NONE', *, *, #23688, .F. ) ;
#4605=ORIENTED_EDGE ( 'NONE', *, *, #62718, .F. ) ;
#4606=VECTOR ( 'NONE', #77015, 1000.000000000000227 ) ;
#4608=CARTESIAN_POINT ( 'NONE',  ( 27.72281430457040940, -21.72500000000000142, 5.000000000000000000 ) ) ;
#4609=DIRECTION ( 'NONE',  ( 0.6830127018922180770, -0.6830127018922204085, -0.2588190451025213501 ) ) ;
#4611=LINE ( 'NONE', #60530, #18680 ) ;
#4612=EDGE_CURVE ( 'NONE', #81346, #125922, #99682, .T. ) ;
#4613=ADVANCED_FACE ( 'NONE', ( #49565 ), #115453, .T. ) ;
#4614=LINE ( 'NONE', #57674, #22076 ) ;
#4615=VERTEX_POINT ( 'NONE', #76624 ) ;
#4617=CARTESIAN_POINT ( 'NONE',  ( -11.20003122016829877, 8.259292476615627265, 16.85664084051843403 ) ) ;
#4618=DIRECTION ( 'NONE',  ( 0.3543493200069163240, -0.000000000000000000, -0.9351131265310288487 ) ) ;
#4619=VECTOR ( 'NONE', #47658, 1000.000000000000000 ) ;
#4620=CARTESIAN_POINT ( 'NONE',  ( 27.79289321881326202, -8.240707523384200428, 5.000000000000000000 ) ) ;
#4622=EDGE_CURVE ( 'NONE', #84037, #6566, #21508, .T. ) ;
#4623=VERTEX_POINT ( 'NONE', #132448 ) ;
#4624=ADVANCED_FACE ( 'NONE', ( #43977 ), #78044, .F. ) ;
#4625=ORIENTED_EDGE ( 'NONE', *, *, #897, .F. ) ;
#4626=ADVANCED_FACE ( 'NONE', ( #54171 ), #98359, .F. ) ;
#4628=DIRECTION ( 'NONE',  ( -0.7071067811865487940, 0.7071067811865463515, -0.000000000000000000 ) ) ;
#4629=CARTESIAN_POINT ( 'NONE',  ( 29.01088028653927964, -22.02621442084248216, 4.990779571109221990 ) ) ;
#4630=EDGE_CURVE ( 'NONE', #38512, #37121, #43271, .T. ) ;
#4632=CARTESIAN_POINT ( 'NONE',  ( -28.49999999999980460, 22.01701374228153085, 2.453858888625695567 ) ) ;
#4633=ORIENTED_EDGE ( 'NONE', *, *, #124622, .F. ) ;
#4634=VERTEX_POINT ( 'NONE', #130993 ) ;
#4635=EDGE_CURVE ( 'NONE', #14634, #85340, #65765, .T. ) ;
#4636=LINE ( 'NONE', #7540, #491 ) ;
#4637=DIRECTION ( 'NONE',  ( 0.7071067811865487940, -0.7071067811865463515, 0.000000000000000000 ) ) ;
#4638=VECTOR ( 'NONE', #33883, 1000.000000000000227 ) ;
#4639=VECTOR ( 'NONE', #5043, 1000.000000000000000 ) ;
#4640=ADVANCED_FACE ( 'NONE', ( #87480 ), #88198, .F. ) ;
#4641=VECTOR ( 'NONE', #46925, 1000.000000000000000 ) ;
#4642=ORIENTED_EDGE ( 'NONE', *, *, #12251, .F. ) ;
#4643=DIRECTION ( 'NONE',  ( 0.7071067811865487940, 0.7071067811865463515, 0.000000000000000000 ) ) ;
#4646=DIRECTION ( 'NONE',  ( -0.7071067811865487940, 0.7071067811865463515, -0.000000000000000000 ) ) ;
#4647=DIRECTION ( 'NONE',  ( 0.7071067811865487940, 0.7071067811865463515, 0.000000000000000000 ) ) ;
#4648=VECTOR ( 'NONE', #109430, 1000.000000000000000 ) ;
#4650=AXIS2_PLACEMENT_3D ( 'NONE', #35322, #68654, #89663 ) ;
#4651=VECTOR ( 'NONE', #74805, 1000.000000000000000 ) ;
#4653=VECTOR ( 'NONE', #9535, 1000.000000000000000 ) ;
#4654=EDGE_CURVE ( 'NONE', #37030, #64397, #143272, .T. ) ;
#4655=FACE_BOUND ( 'NONE', #116935, .T. ) ;
#4656=CARTESIAN_POINT ( 'NONE',  ( -37.62823445044362103, -8.240707523384193323, 11.38925528200761228 ) ) ;
#4657=CARTESIAN_POINT ( 'NONE',  ( 3.722814304570581712, -21.72499999999999432, 5.000000000000000000 ) ) ;
#4658=DIRECTION ( 'NONE',  ( 0.7071067811865487940, 0.7071067811865463515, 0.000000000000000000 ) ) ;
#4660=EDGE_CURVE ( 'NONE', #11497, #105889, #121509, .T. ) ;
#4661=PLANE ( 'NONE',  #53283 ) ;
#4664=ORIENTED_EDGE ( 'NONE', *, *, #43389, .F. ) ;
#4666=ORIENTED_EDGE ( 'NONE', *, *, #62977, .F. ) ;
#4669=PLANE ( 'NONE',  #107200 ) ;
#4670=DIRECTION ( 'NONE',  ( -0.7071067811865486830, -0.7071067811865464625, 0.000000000000000000 ) ) ;
#4671=AXIS2_PLACEMENT_3D ( 'NONE', #86380, #106660, #73365 ) ;
#4672=CARTESIAN_POINT ( 'NONE',  ( -34.92500000000001137, -13.91861162105994332, 18.69616556237236793 ) ) ;
#4673=EDGE_CURVE ( 'NONE', #132626, #23262, #51447, .T. ) ;
#4674=EDGE_LOOP ( 'NONE', ( #48934, #60606, #68508, #139843 ) ) ;
#4675=CARTESIAN_POINT ( 'NONE',  ( 11.99999999999991473, -9.033600742197648970, 5.000000000000000000 ) ) ;
#4676=VECTOR ( 'NONE', #51651, 999.9999999999998863 ) ;
#4678=CARTESIAN_POINT ( 'NONE',  ( -26.99999999999981171, 8.966399257802175171, 5.000000000000000000 ) ) ;
#4679=LINE ( 'NONE', #125825, #105951 ) ;
#4680=DIRECTION ( 'NONE',  ( -0.6830127018922181881, 0.6830127018922202975, -0.2588190451025214056 ) ) ;
#4681=EDGE_CURVE ( 'NONE', #117376, #103116, #99766, .T. ) ;
#4682=LINE ( 'NONE', #91069, #120166 ) ;
#4683=CARTESIAN_POINT ( 'NONE',  ( -22.49999999999983658, 10.08746187583913922, 4.000000000000000000 ) ) ;
#4684=ORIENTED_EDGE ( 'NONE', *, *, #105664, .F. ) ;
#4685=AXIS2_PLACEMENT_3D ( 'NONE', #13349, #35156, #67803 ) ;
#4686=CARTESIAN_POINT ( 'NONE',  ( 34.49999999999975842, -1.535744391599495273, 4.994342998332161443 ) ) ;
#4687=EDGE_CURVE ( 'NONE', #13443, #120930, #59168, .T. ) ;
#4689=ORIENTED_EDGE ( 'NONE', *, *, #29115, .T. ) ;
#4690=EDGE_LOOP ( 'NONE', ( #11672, #66259, #141755, #18964 ) ) ;
#4691=ORIENTED_EDGE ( 'NONE', *, *, #123821, .F. ) ;
#4693=ORIENTED_EDGE ( 'NONE', *, *, #59004, .T. ) ;
#4694=EDGE_CURVE ( 'NONE', #31169, #33404, #35267, .T. ) ;
#4695=VECTOR ( 'NONE', #118557, 1000.000000000000000 ) ;
#4698=ORIENTED_EDGE ( 'NONE', *, *, #53683, .F. ) ;
#4699=EDGE_CURVE ( 'NONE', #87818, #139479, #70051, .T. ) ;
#4700=DIRECTION ( 'NONE',  ( 0.7071067811865487940, -0.7071067811865463515, 0.000000000000000000 ) ) ;
#4701=VERTEX_POINT ( 'NONE', #47582 ) ;
#4702=FACE_OUTER_BOUND ( 'NONE', #93176, .T. ) ;
#4704=CARTESIAN_POINT ( 'NONE',  ( 22.49999999999984723, 12.05218569542904739, 5.000000000000000000 ) ) ;
#4705=ORIENTED_EDGE ( 'NONE', *, *, #55667, .F. ) ;
#4706=ORIENTED_EDGE ( 'NONE', *, *, #82969, .F. ) ;
#4707=CARTESIAN_POINT ( 'NONE',  ( -32.29289321881321939, -18.74070752338409207, 5.000000000000000000 ) ) ;
#4709=ORIENTED_EDGE ( 'NONE', *, *, #84426, .T. ) ;
#4710=CARTESIAN_POINT ( 'NONE',  ( 33.48921356237309510, -27.52281430457078670, 5.000000000000000000 ) ) ;
#4711=ORIENTED_EDGE ( 'NONE', *, *, #95825, .F. ) ;
#4712=EDGE_LOOP ( 'NONE', ( #70478, #32398, #61624, #29877 ) ) ;
#4713=EDGE_CURVE ( 'NONE', #39610, #90585, #114213, .T. ) ;
#4714=EDGE_LOOP ( 'NONE', ( #88066, #17537, #89064, #76430 ) ) ;
#4715=ORIENTED_EDGE ( 'NONE', *, *, #3295, .T. ) ;
#4716=CARTESIAN_POINT ( 'NONE',  ( -24.32816939922335919, -15.74070752338412049, 4.000000000000000000 ) ) ;
#4719=CARTESIAN_POINT ( 'NONE',  ( 33.48921356237309510, -27.52281430457078670, 5.000000000000000000 ) ) ;
#4720=EDGE_CURVE ( 'NONE', #6614, #24067, #135289, .T. ) ;
#4721=DIRECTION ( 'NONE',  ( -0.3543493200069162685, -0.000000000000000000, -0.9351131265310288487 ) ) ;
#4722=DIRECTION ( 'NONE',  ( -0.000000000000000000, -0.3543493200069152693, 0.9351131265310292928 ) ) ;
#4723=ORIENTED_EDGE ( 'NONE', *, *, #120226, .F. ) ;
#4724=AXIS2_PLACEMENT_3D ( 'NONE', #114124, #92351, #137322 ) ;
#4726=DIRECTION ( 'NONE',  ( 0.6830127018922181881, 0.6830127018922202975, -0.2588190451025214056 ) ) ;
#4729=DIRECTION ( 'NONE',  ( 1.000000000000000000, 0.000000000000000000, 0.000000000000000000 ) ) ;
#4730=DIRECTION ( 'NONE',  ( 0.3543493200069162685, -0.000000000000000000, -0.9351131265310288487 ) ) ;
#4732=VERTEX_POINT ( 'NONE', #104018 ) ;
#4733=ORIENTED_EDGE ( 'NONE', *, *, #28340, .T. ) ;
#4734=EDGE_LOOP ( 'NONE', ( #66650, #123584, #135024 ) ) ;
#4737=FACE_OUTER_BOUND ( 'NONE', #105094, .T. ) ;
#4738=LINE ( 'NONE', #57789, #82167 ) ;
#4739=VECTOR ( 'NONE', #121161, 1000.000000000000000 ) ;
#4740=DIRECTION ( 'NONE',  ( -0.000000000000000000, -0.3543493200069152693, 0.9351131265310292928 ) ) ;
#4742=EDGE_CURVE ( 'NONE', #26904, #26060, #67911, .T. ) ;
#4743=CARTESIAN_POINT ( 'NONE',  ( -11.99999999999992006, 7.588810512006196163, -3.013526669885200793 ) ) ;
#4746=CARTESIAN_POINT ( 'NONE',  ( -8.510786437626906675, -27.52281430457049183, 5.000000000000000000 ) ) ;
#4748=CARTESIAN_POINT ( 'NONE',  ( -33.70710678118631165, -12.74070752338415602, 5.000000000000000000 ) ) ;
#4749=LINE ( 'NONE', #104092, #25812 ) ;
#4750=DIRECTION ( 'NONE',  ( 0.7071067811865487940, 0.7071067811865463515, 0.000000000000000000 ) ) ;
#4751=EDGE_LOOP ( 'NONE', ( #110759, #50963, #124654, #53214, #112307 ) ) ;
#4752=VECTOR ( 'NONE', #15985, 999.9999999999998863 ) ;
#4754=AXIS2_PLACEMENT_3D ( 'NONE', #75786, #7635, #94645 ) ;
#4755=VECTOR ( 'NONE', #88807, 1000.000000000000000 ) ;
#4756=CARTESIAN_POINT ( 'NONE',  ( -23.81601139373100295, 28.73617430169770870, 5.000000000000000000 ) ) ;
#4757=ORIENTED_EDGE ( 'NONE', *, *, #48946, .T. ) ;
#4758=VECTOR ( 'NONE', #32234, 1000.000000000000114 ) ;
#4759=CARTESIAN_POINT ( 'NONE',  ( -18.70710678118641468, 17.25929247661554200, 5.000000000000000000 ) ) ;
#4760=CARTESIAN_POINT ( 'NONE',  ( 34.47516574401890921, -16.50948238788420852, 4.998110765256833510 ) ) ;
#4761=VERTEX_POINT ( 'NONE', #13447 ) ;
#4762=EDGE_CURVE ( 'NONE', #92431, #8931, #68597, .T. ) ;
#4763=CARTESIAN_POINT ( 'NONE',  ( 26.48334561358936412, 22.22500000000000142, 4.500000000000000888 ) ) ;
#4765=ORIENTED_EDGE ( 'NONE', *, *, #18418, .T. ) ;
#4766=CARTESIAN_POINT ( 'NONE',  ( 0.000000000000000000, 0.000000000000000000, 5.000000000000000000 ) ) ;
#4767=EDGE_LOOP ( 'NONE', ( #420, #35815, #13612, #55957 ) ) ;
#4768=DIRECTION ( 'NONE',  ( -0.7071067811865486830, -0.7071067811865464625, 0.000000000000000000 ) ) ;
#4770=VERTEX_POINT ( 'NONE', #37380 ) ;
#4771=DIRECTION ( 'NONE',  ( -0.000000000000000000, 0.3543493200069153248, 0.9351131265310292928 ) ) ;
#4773=LINE ( 'NONE', #114301, #60213 ) ;
#4774=PLANE ( 'NONE',  #143303 ) ;
#4775=ORIENTED_EDGE ( 'NONE', *, *, #37968, .T. ) ;
#4776=AXIS2_PLACEMENT_3D ( 'NONE', #125623, #48774, #116151 ) ;
#4777=DIRECTION ( 'NONE',  ( -0.7071067811865486830, 0.7071067811865464625, 0.000000000000000000 ) ) ;
#4778=PLANE ( 'NONE',  #62322 ) ;
#4780=CARTESIAN_POINT ( 'NONE',  ( 72.48921356237309510, -27.52281430457106026, 5.000000000000000000 ) ) ;
#4782=PLANE ( 'NONE',  #129969 ) ;
#4783=ORIENTED_EDGE ( 'NONE', *, *, #125439, .F. ) ;
#4784=AXIS2_PLACEMENT_3D ( 'NONE', #136833, #137564, #15716 ) ;
#4785=DIRECTION ( 'NONE',  ( 1.000000000000000000, 0.000000000000000000, 0.000000000000000000 ) ) ;
#4786=VERTEX_POINT ( 'NONE', #81619 ) ;
#4787=VECTOR ( 'NONE', #108970, 1000.000000000000000 ) ;
#4789=CARTESIAN_POINT ( 'NONE',  ( -8.999999999999937828, -10.77435723561695902, -9.972017380717208113 ) ) ;
#4790=EDGE_CURVE ( 'NONE', #121707, #85225, #4679, .T. ) ;
#4791=DIRECTION ( 'NONE',  ( 0.7071067811865487940, 0.7071067811865463515, 0.000000000000000000 ) ) ;
#4792=FACE_OUTER_BOUND ( 'NONE', #15066, .T. ) ;
#4793=ORIENTED_EDGE ( 'NONE', *, *, #93459, .F. ) ;
#4794=AXIS2_PLACEMENT_3D ( 'NONE', #706, #66018, #131243 ) ;
#4795=CARTESIAN_POINT ( 'NONE',  ( -45.48921356237309510, -27.52281430457087197, 5.000000000000000000 ) ) ;
#4796=CARTESIAN_POINT ( 'NONE',  ( -34.92500000000001137, 1.512461875839480552, 4.000000000000000000 ) ) ;
#4797=CARTESIAN_POINT ( 'NONE',  ( 23.99451991528749062, 28.92564299267954908, 4.000000000000000000 ) ) ;
#4799=DIRECTION ( 'NONE',  ( 0.7071067811865487940, -0.7071067811865463515, 0.000000000000000000 ) ) ;
#4800=LINE ( 'NONE', #136083, #123848 ) ;
#4801=ORIENTED_EDGE ( 'NONE', *, *, #5928, .F. ) ;
#4802=LINE ( 'NONE', #115008, #20567 ) ;
#4803=DIRECTION ( 'NONE',  ( -0.7071067811865486830, 0.7071067811865464625, 0.000000000000000000 ) ) ;
#4805=CARTESIAN_POINT ( 'NONE',  ( 45.18398860626900415, 28.73617430169818832, 5.000000000000000000 ) ) ;
#4806=VERTEX_POINT ( 'NONE', #70745 ) ;
#4808=VERTEX_POINT ( 'NONE', #48979 ) ;
#4809=ADVANCED_FACE ( 'NONE', ( #137409 ), #134569, .F. ) ;
#4812=EDGE_LOOP ( 'NONE', ( #105292, #1071, #59042, #72547 ) ) ;
#4813=ADVANCED_FACE ( 'NONE', ( #130655 ), #138117, .F. ) ;
#4815=CARTESIAN_POINT ( 'NONE',  ( -4.828169399223493308, -20.24070752338407431, 4.000000000000000000 ) ) ;
#4817=AXIS2_PLACEMENT_3D ( 'NONE', #44668, #1087, #82110 ) ;
#4818=LINE ( 'NONE', #115024, #1695 ) ;
#4820=ORIENTED_EDGE ( 'NONE', *, *, #45308, .F. ) ;
#4821=VECTOR ( 'NONE', #121743, 1000.000000000000000 ) ;
#4823=CARTESIAN_POINT ( 'NONE',  ( 75.18398860626899705, 28.73617430169839793, 5.000000000000000000 ) ) ;
#4824=LINE ( 'NONE', #16438, #32892 ) ;
#4825=ORIENTED_EDGE ( 'NONE', *, *, #119211, .T. ) ;
#4826=EDGE_CURVE ( 'NONE', #124937, #24394, #54519, .T. ) ;
#4827=CARTESIAN_POINT ( 'NONE',  ( -69.18398860626899705, 28.73617430169835529, 5.000000000000000000 ) ) ;
#4828=PLANE ( 'NONE',  #64045 ) ;
#4832=ORIENTED_EDGE ( 'NONE', *, *, #81920, .T. ) ;
#4833=EDGE_CURVE ( 'NONE', #117516, #62013, #142243, .T. ) ;
#4837=DIRECTION ( 'NONE',  ( -0.7071067811865486830, -0.7071067811865464625, 0.000000000000000000 ) ) ;
#4838=DIRECTION ( 'NONE',  ( 0.7071067811865487940, 0.7071067811865463515, 0.000000000000000000 ) ) ;
#4839=VECTOR ( 'NONE', #21057, 1000.000000000000000 ) ;
#4840=DIRECTION ( 'NONE',  ( -0.7071067811865486830, -0.7071067811865464625, 0.000000000000000000 ) ) ;
#4842=PLANE ( 'NONE',  #34871 ) ;
#4843=DIRECTION ( 'NONE',  ( 0.6830127018922181881, 0.6830127018922202975, -0.2588190451025214056 ) ) ;
#4845=ORIENTED_EDGE ( 'NONE', *, *, #104548, .F. ) ;
#4846=EDGE_LOOP ( 'NONE', ( #143192, #120180, #103402, #19787 ) ) ;
#4847=ORIENTED_EDGE ( 'NONE', *, *, #19629, .T. ) ;
#4848=VECTOR ( 'NONE', #9377, 1000.000000000000000 ) ;
#4850=VECTOR ( 'NONE', #111353, 1000.000000000000000 ) ;
#4851=VECTOR ( 'NONE', #84608, 1000.000000000000000 ) ;
#4854=CARTESIAN_POINT ( 'NONE',  ( -18.48921356237309510, -27.52281430457068367, 5.000000000000000000 ) ) ;
#4855=CARTESIAN_POINT ( 'NONE',  ( 51.18398860626899705, 28.73617430169823095, 5.000000000000000000 ) ) ;
#4856=LINE ( 'NONE', #17215, #131362 ) ;
#4857=EDGE_CURVE ( 'NONE', #65916, #20734, #119028, .T. ) ;
#4858=CARTESIAN_POINT ( 'NONE',  ( -30.48921356237309510, -27.52281430457076894, 5.000000000000000000 ) ) ;
#4859=VECTOR ( 'NONE', #60490, 1000.000000000000227 ) ;
#4860=VECTOR ( 'NONE', #69626, 1000.000000000000000 ) ;
#4861=PLANE ( 'NONE',  #16623 ) ;
#4862=ORIENTED_EDGE ( 'NONE', *, *, #87078, .T. ) ;
#4863=AXIS2_PLACEMENT_3D ( 'NONE', #7424, #29900, #104617 ) ;
#4864=LINE ( 'NONE', #38267, #26349 ) ;
#4865=DIRECTION ( 'NONE',  ( -0.3543493200069162685, -0.000000000000000000, -0.9351131265310288487 ) ) ;
#4866=ORIENTED_EDGE ( 'NONE', *, *, #68990, .F. ) ;
#4867=PLANE ( 'NONE',  #89890 ) ;
#4868=ORIENTED_EDGE ( 'NONE', *, *, #4152, .F. ) ;
#4869=ORIENTED_EDGE ( 'NONE', *, *, #126938, .F. ) ;
#4870=LINE ( 'NONE', #13636, #126922 ) ;
#4871=ORIENTED_EDGE ( 'NONE', *, *, #110987, .F. ) ;
#4873=AXIS2_PLACEMENT_3D ( 'NONE', #124151, #79980, #135069 ) ;
#4875=VERTEX_POINT ( 'NONE', #87126 ) ;
#4876=EDGE_CURVE ( 'NONE', #13143, #22841, #63955, .T. ) ;
#4877=CARTESIAN_POINT ( 'NONE',  ( 10.49999999999992539, -17.56887692260763245, 4.000000000000000000 ) ) ;
#4878=CARTESIAN_POINT ( 'NONE',  ( -34.42500000000001137, -21.72500000000000142, 0.5000000000000000000 ) ) ;
#4880=DIRECTION ( 'NONE',  ( 0.7071067811865486830, -0.7071067811865464625, -0.000000000000000000 ) ) ;
#4881=AXIS2_PLACEMENT_3D ( 'NONE', #81237, #125441, #48585 ) ;
#4882=EDGE_CURVE ( 'NONE', #77399, #102312, #27195, .T. ) ;
#4883=CARTESIAN_POINT ( 'NONE',  ( 6.792893218813413014, -2.240707523384257716, 5.000000000000000000 ) ) ;
#4884=PLANE ( 'NONE',  #83766 ) ;
#4885=DIRECTION ( 'NONE',  ( 0.7071067811865487940, 0.7071067811865463515, 0.000000000000000000 ) ) ;
#4886=CARTESIAN_POINT ( 'NONE',  ( 15.98155265364320599, 18.75929247661552424, 20.33588619593439617 ) ) ;
#4887=CARTESIAN_POINT ( 'NONE',  ( 0.000000000000000000, 0.000000000000000000, 5.000000000000000000 ) ) ;
#4888=VECTOR ( 'NONE', #71792, 999.9999999999998863 ) ;
#4889=VERTEX_POINT ( 'NONE', #105458 ) ;
#4890=VECTOR ( 'NONE', #118801, 1000.000000000000000 ) ;
#4892=EDGE_CURVE ( 'NONE', #120044, #21301, #98699, .T. ) ;
#4893=EDGE_LOOP ( 'NONE', ( #25214, #21585, #93354, #119818 ) ) ;
#4894=VECTOR ( 'NONE', #12759, 1000.000000000000000 ) ;
#4895=ORIENTED_EDGE ( 'NONE', *, *, #8146, .F. ) ;
#4896=DIRECTION ( 'NONE',  ( -0.000000000000000000, -0.3543493200069152693, 0.9351131265310292928 ) ) ;
#4897=EDGE_LOOP ( 'NONE', ( #37398, #25632, #42473, #5261 ) ) ;
#4898=VECTOR ( 'NONE', #87570, 1000.000000000000000 ) ;
#4899=CARTESIAN_POINT ( 'NONE',  ( -1.499999999999994449, -11.56887692260769462, 4.000000000000000000 ) ) ;
#4900=CARTESIAN_POINT ( 'NONE',  ( 42.29974487139158157, -27.71228299555235708, 4.000000000000000000 ) ) ;
#4901=EDGE_CURVE ( 'NONE', #118694, #63182, #22629, .T. ) ;
#4902=AXIS2_PLACEMENT_3D ( 'NONE', #131416, #32095, #98758 ) ;
#4903=CARTESIAN_POINT ( 'NONE',  ( -24.18398860626899705, 28.73617430169804265, 5.000000000000000000 ) ) ;
#4905=ORIENTED_EDGE ( 'NONE', *, *, #20259, .T. ) ;
#4907=ORIENTED_EDGE ( 'NONE', *, *, #40155, .F. ) ;
#4909=VECTOR ( 'NONE', #99023, 999.9999999999998863 ) ;
#4911=CARTESIAN_POINT ( 'NONE',  ( -11.58838509405160089, 22.22500000000000142, 4.777194822843815025 ) ) ;
#4912=CARTESIAN_POINT ( 'NONE',  ( 16.82816939922340893, -14.24070752338414003, 4.000000000000000000 ) ) ;
#4914=ORIENTED_EDGE ( 'NONE', *, *, #59458, .F. ) ;
#4915=ORIENTED_EDGE ( 'NONE', *, *, #6267, .T. ) ;
#4917=VERTEX_POINT ( 'NONE', #138840 ) ;
#4918=CARTESIAN_POINT ( 'NONE',  ( -34.91764015037184521, 21.81495039010403048, 4.089230673112417058 ) ) ;
#4919=LINE ( 'NONE', #71667, #76558 ) ;
#4920=DIRECTION ( 'NONE',  ( 0.6830127018922181881, 0.6830127018922202975, -0.2588190451025214056 ) ) ;
#4921=VECTOR ( 'NONE', #11358, 1000.000000000000000 ) ;
#4922=CARTESIAN_POINT ( 'NONE',  ( 21.32816939922338051, 17.25929247661554911, 4.000000000000000000 ) ) ;
#4923=DIRECTION ( 'NONE',  ( 0.000000000000000000, -0.3543493200069152138, 0.9351131265310292928 ) ) ;
#4924=CARTESIAN_POINT ( 'NONE',  ( 60.48921356237309510, -27.52281430457097500, 5.000000000000000000 ) ) ;
#4925=LINE ( 'NONE', #128201, #16204 ) ;
#4927=CARTESIAN_POINT ( 'NONE',  ( -34.92500000000001137, 21.72500000000000142, 5.000000000000000000 ) ) ;
#4928=EDGE_CURVE ( 'NONE', #25784, #79543, #16298, .T. ) ;
#4929=LINE ( 'NONE', #69557, #99758 ) ;
#4930=ORIENTED_EDGE ( 'NONE', *, *, #59542, .T. ) ;
#4931=LINE ( 'NONE', #73812, #108805 ) ;
#4932=DIRECTION ( 'NONE',  ( -0.7071067811865486830, -0.7071067811865464625, 0.000000000000000000 ) ) ;
#4933=VERTEX_POINT ( 'NONE', #41462 ) ;
#4934=DIRECTION ( 'NONE',  ( -0.7071067811865486830, -0.7071067811865464625, 0.000000000000000000 ) ) ;
#4935=ADVANCED_FACE ( 'NONE', ( #129913 ), #30622, .T. ) ;
#4936=EDGE_LOOP ( 'NONE', ( #118566, #49439, #35449 ) ) ;
#4937=ORIENTED_EDGE ( 'NONE', *, *, #118742, .F. ) ;
#4938=EDGE_CURVE ( 'NONE', #92320, #48278, #68271, .T. ) ;
#4939=DIRECTION ( 'NONE',  ( 0.7071067811865486830, -0.7071067811865464625, -0.000000000000000000 ) ) ;
#4940=CARTESIAN_POINT ( 'NONE',  ( 27.18398860626900060, 28.73617430169806042, 5.000000000000000000 ) ) ;
#4941=PLANE ( 'NONE',  #71498 ) ;
#4943=ORIENTED_EDGE ( 'NONE', *, *, #37089, .T. ) ;
#4944=CARTESIAN_POINT ( 'NONE',  ( 3.489213562373097322, -27.52281430457057709, 5.000000000000000000 ) ) ;
#4946=CARTESIAN_POINT ( 'NONE',  ( -3.183988606268992161, 28.73617430169789699, 5.000000000000000000 ) ) ;
#4947=CARTESIAN_POINT ( 'NONE',  ( 2.999999999999985345, 14.58746187583909837, 4.000000000000000000 ) ) ;
#4949=PLANE ( 'NONE',  #32364 ) ;
#4950=PLANE ( 'NONE',  #50918 ) ;
#4953=CARTESIAN_POINT ( 'NONE',  ( -50.99451991528749062, 28.92564299267973738, 4.000000000000000000 ) ) ;
#4956=LINE ( 'NONE', #17983, #78343 ) ;
#4957=VECTOR ( 'NONE', #128029, 1000.000000000000000 ) ;
#4958=AXIS2_PLACEMENT_3D ( 'NONE', #61170, #27762, #8125 ) ;
#4960=CARTESIAN_POINT ( 'NONE',  ( -25.39656807105341585, -14.24070752338413648, 19.24067776001720276 ) ) ;
#4962=EDGE_CURVE ( 'NONE', #110890, #87848, #134207, .T. ) ;
#4966=AXIS2_PLACEMENT_3D ( 'NONE', #39517, #15549, #61299 ) ;
#4967=VERTEX_POINT ( 'NONE', #24013 ) ;
#4968=ORIENTED_EDGE ( 'NONE', *, *, #9052, .T. ) ;
#4969=DIRECTION ( 'NONE',  ( 0.7071067811865487940, 0.7071067811865463515, 0.000000000000000000 ) ) ;
#4970=DIRECTION ( 'NONE',  ( -0.6830127018922180770, -0.6830127018922204085, -0.2588190451025213501 ) ) ;
#4972=AXIS2_PLACEMENT_3D ( 'NONE', #40516, #18716, #43364 ) ;
#4973=VECTOR ( 'NONE', #97711, 999.9999999999998863 ) ;
#4974=VECTOR ( 'NONE', #42535, 1000.000000000000000 ) ;
#4975=DIRECTION ( 'NONE',  ( -0.6830127018922180770, -0.6830127018922204085, -0.2588190451025213501 ) ) ;
#4976=ORIENTED_EDGE ( 'NONE', *, *, #117660, .F. ) ;
#4977=CARTESIAN_POINT ( 'NONE',  ( 19.49999999999986855, -2.947814304570800736, 5.000000000000000000 ) ) ;
#4978=VECTOR ( 'NONE', #128361, 999.9999999999998863 ) ;
#4979=DIRECTION ( 'NONE',  ( 0.7071067811865487940, 0.7071067811865463515, 0.000000000000000000 ) ) ;
#4983=CARTESIAN_POINT ( 'NONE',  ( 34.92499999999998295, 15.75929247661555799, 4.255531930566167631 ) ) ;
#4985=LINE ( 'NONE', #115178, #70700 ) ;
#4986=DIRECTION ( 'NONE',  ( 1.000000000000000000, 0.000000000000000000, 0.000000000000000000 ) ) ;
#4987=FACE_OUTER_BOUND ( 'NONE', #112065, .T. ) ;
#4988=FACE_OUTER_BOUND ( 'NONE', #136907, .T. ) ;
#4989=ORIENTED_EDGE ( 'NONE', *, *, #9632, .F. ) ;
#4991=EDGE_CURVE ( 'NONE', #100625, #72772, #21859, .T. ) ;
#4994=EDGE_CURVE ( 'NONE', #50737, #5604, #132808, .T. ) ;
#4995=LINE ( 'NONE', #83330, #119465 ) ;
#4996=ORIENTED_EDGE ( 'NONE', *, *, #12227, .T. ) ;
#4997=EDGE_CURVE ( 'NONE', #97211, #48429, #13106, .T. ) ;
#4998=ADVANCED_FACE ( 'NONE', ( #11664 ), #87833, .F. ) ;
#4999=FACE_OUTER_BOUND ( 'NONE', #90771, .T. ) ;
#5001=VECTOR ( 'NONE', #142220, 1000.000000000000227 ) ;
#5002=AXIS2_PLACEMENT_3D ( 'NONE', #82997, #40230, #17020 ) ;
#5004=ORIENTED_EDGE ( 'NONE', *, *, #11407, .T. ) ;
#5005=VECTOR ( 'NONE', #84320, 1000.000000000000227 ) ;
#5006=LINE ( 'NONE', #137729, #109029 ) ;
#5007=ORIENTED_EDGE ( 'NONE', *, *, #60542, .T. ) ;
#5008=DIRECTION ( 'NONE',  ( -0.000000000000000000, -0.3543493200069152693, 0.9351131265310292928 ) ) ;
#5010=VECTOR ( 'NONE', #109685, 1000.000000000000000 ) ;
#5011=CARTESIAN_POINT ( 'NONE',  ( 32.20666063542130075, 21.75929247661549937, 4.998822639870702744 ) ) ;
#5012=ORIENTED_EDGE ( 'NONE', *, *, #123732, .T. ) ;
#5014=EDGE_CURVE ( 'NONE', #70001, #22050, #132075, .T. ) ;
#5015=EDGE_LOOP ( 'NONE', ( #5266, #52642, #35865, #42399 ) ) ;
#5016=CARTESIAN_POINT ( 'NONE',  ( -21.65671000166199889, 3.759292476615678336, 13.27625715073260615 ) ) ;
#5017=EDGE_CURVE ( 'NONE', #71118, #141981, #23265, .T. ) ;
#5018=CARTESIAN_POINT ( 'NONE',  ( -18.29974487139159223, -27.71228299555219010, 4.000000000000000000 ) ) ;
#5020=VECTOR ( 'NONE', #139567, 999.9999999999998863 ) ;
#5022=EDGE_CURVE ( 'NONE', #97224, #124154, #2208, .T. ) ;
#5023=CARTESIAN_POINT ( 'NONE',  ( 15.29974487139158867, -27.71228299555216879, 4.000000000000000000 ) ) ;
#5024=ORIENTED_EDGE ( 'NONE', *, *, #57313, .F. ) ;
#5026=DIRECTION ( 'NONE',  ( -0.3543493200069162685, -0.000000000000000000, -0.9351131265310288487 ) ) ;
#5027=ORIENTED_EDGE ( 'NONE', *, *, #30389, .F. ) ;
#5029=AXIS2_PLACEMENT_3D ( 'NONE', #101497, #125411, #48559 ) ;
#5031=VECTOR ( 'NONE', #85747, 1000.000000000000000 ) ;
#5032=DIRECTION ( 'NONE',  ( 0.7071067811865487940, -0.7071067811865463515, 0.000000000000000000 ) ) ;
#5033=PLANE ( 'NONE',  #134519 ) ;
#5034=CARTESIAN_POINT ( 'NONE',  ( 21.80077440930739030, -2.123201397992801276, 4.669108085256719498 ) ) ;
#5035=ORIENTED_EDGE ( 'NONE', *, *, #86316, .F. ) ;
#5036=CARTESIAN_POINT ( 'NONE',  ( -51.48921356237309510, -27.52281430457091460, 5.000000000000000000 ) ) ;
#5038=ADVANCED_FACE ( 'NONE', ( #90710 ), #121865, .F. ) ;
#5039=VECTOR ( 'NONE', #142806, 1000.000000000000227 ) ;
#5040=DIRECTION ( 'NONE',  ( -2.781805975412905890E-17, 0.3543493200069152693, 0.9351131265310292928 ) ) ;
#5041=CARTESIAN_POINT ( 'NONE',  ( 69.18398860626899705, 28.73617430169835529, 5.000000000000000000 ) ) ;
#5042=ORIENTED_EDGE ( 'NONE', *, *, #23885, .F. ) ;
#5043=DIRECTION ( 'NONE',  ( 0.7071067811865486830, -0.7071067811865464625, -0.000000000000000000 ) ) ;
#5044=FACE_BOUND ( 'NONE', #4353, .T. ) ;
#5045=ORIENTED_EDGE ( 'NONE', *, *, #139599, .F. ) ;
#5046=LINE ( 'NONE', #127587, #18013 ) ;
#5047=FACE_OUTER_BOUND ( 'NONE', #84772, .T. ) ;
#5050=EDGE_CURVE ( 'NONE', #10646, #130556, #79865, .T. ) ;
#5051=CARTESIAN_POINT ( 'NONE',  ( -12.48921356237309155, -27.52281430457064104, 5.000000000000000000 ) ) ;
#5052=EDGE_LOOP ( 'NONE', ( #34752, #109750, #16074, #88777 ) ) ;
#5053=EDGE_CURVE ( 'NONE', #114924, #119580, #110275, .T. ) ;
#5054=ORIENTED_EDGE ( 'NONE', *, *, #56782, .F. ) ;
#5056=ORIENTED_EDGE ( 'NONE', *, *, #119766, .F. ) ;
#5057=EDGE_CURVE ( 'NONE', #104233, #53420, #110982, .T. ) ;
#5059=ORIENTED_EDGE ( 'NONE', *, *, #104423, .T. ) ;
#5060=DIRECTION ( 'NONE',  ( -1.000000000000000000, 0.000000000000000000, 0.000000000000000000 ) ) ;
#5061=CARTESIAN_POINT ( 'NONE',  ( -18.29974487139159223, -27.71228299555219010, 4.000000000000000000 ) ) ;
#5064=DIRECTION ( 'NONE',  ( -0.6830127018922180770, -0.6830127018922204085, -0.2588190451025213501 ) ) ;
#5066=VECTOR ( 'NONE', #121188, 1000.000000000000000 ) ;
#5067=VECTOR ( 'NONE', #73198, 1000.000000000000227 ) ;
#5068=AXIS2_PLACEMENT_3D ( 'NONE', #42939, #87139, #131356 ) ;
#5069=AXIS2_PLACEMENT_3D ( 'NONE', #21125, #42911, #74835 ) ;
#5070=CARTESIAN_POINT ( 'NONE',  ( 34.82816939922328459, -11.24070752338417201, 4.000000000000000000 ) ) ;
#5071=CARTESIAN_POINT ( 'NONE',  ( 34.04515773336645879, -21.74070752338406365, 21.72585301388592782 ) ) ;
#5072=CARTESIAN_POINT ( 'NONE',  ( 18.29974487139159223, -27.71228299555219010, 4.000000000000000000 ) ) ;
#5073=DIRECTION ( 'NONE',  ( -0.7071067811865486830, 0.7071067811865464625, 0.000000000000000000 ) ) ;
#5074=ORIENTED_EDGE ( 'NONE', *, *, #48069, .F. ) ;
#5075=EDGE_LOOP ( 'NONE', ( #43962, #102032, #21753, #7868, #81885, #110574, #66481, #71563, #88514, #84377, #113352, #35214, #62901, #23789, #945, #61389, #32422, #17877, #138049, #20012, #7582, #26219, #132492, #90114, #48275, #76497, #130553, #17107, #35980, #140198, #51998, #25018, #29237, #75805, #2145, #43933, #79853, #16251, #110508, #65189, #43334, #28756, #34859, #12466, #82071, #37964, #28910, #33171, #112106, #103810, #118441, #65019, #130644, #123819, #7352, #10792, #38255, #21010, #44210, #101201, #35923, #134125, #61518, #129303, #112630, #43540, #125019, #27182, #10834, #653, #91923, #107581, #46083, #130250, #118768, #98053, #76634, #17868, #138778, #113998, #66545, #25420, #28639, #132089, #18113, #124048, #25466, #115707, #55065, #107145, #61627, #101723, #34405, #103476, #81659, #3587, #99349, #11143, #41235, #8021, #28250, #46516, #84487, #57825, #108478, #127543, #131389, #15207, #82547, #78696, #139493, #84761, #32497, #60032, #143120, #117415, #123931, #48519, #123339, #133638, #102849, #53887, #19933, #3506, #87387, #21222, #3346, #112048, #110327, #78204, #29727, #29770, #103652, #7458, #111640, #43577, #45527, #130292, #67937, #111937, #127692, #38860, #100498, #124800, #34356, #137483, #18158, #59908, #86150, #26792, #108111, #21664, #126913, #117587, #9653, #83755, #105306, #136892, #100468, #120161, #108972, #20022, #128549, #14139 ) ) ;
#5076=VECTOR ( 'NONE', #133769, 1000.000000000000000 ) ;
#5077=ORIENTED_EDGE ( 'NONE', *, *, #125803, .F. ) ;
#5079=ORIENTED_EDGE ( 'NONE', *, *, #96343, .F. ) ;
#5081=ORIENTED_EDGE ( 'NONE', *, *, #46857, .F. ) ;
#5082=VERTEX_POINT ( 'NONE', #24712 ) ;
#5083=LINE ( 'NONE', #72578, #51321 ) ;
#5084=ADVANCED_FACE ( 'NONE', ( #100150 ), #122589, .F. ) ;
#5085=CARTESIAN_POINT ( 'NONE',  ( 6.394038684143281692, 22.22500000000000142, 20.65732834419774377 ) ) ;
#5086=ORIENTED_EDGE ( 'NONE', *, *, #50342, .T. ) ;
#5089=DIRECTION ( 'NONE',  ( 0.7071067811865487940, 0.7071067811865463515, 0.000000000000000000 ) ) ;
#5090=CARTESIAN_POINT ( 'NONE',  ( 10.49999999999993605, 13.08746187583911080, 4.000000000000000000 ) ) ;
#5094=CARTESIAN_POINT ( 'NONE',  ( 22.17183060077631396, -17.24070752338410628, 4.000000000000000000 ) ) ;
#5096=LINE ( 'NONE', #61001, #46565 ) ;
#5097=ORIENTED_EDGE ( 'NONE', *, *, #141166, .F. ) ;
#5098=VERTEX_POINT ( 'NONE', #5786 ) ;
#5099=DIRECTION ( 'NONE',  ( 1.000000000000000000, 0.000000000000000000, 0.000000000000000000 ) ) ;
#5100=VERTEX_POINT ( 'NONE', #2952 ) ;
#5101=FACE_OUTER_BOUND ( 'NONE', #25965, .T. ) ;
#5105=ORIENTED_EDGE ( 'NONE', *, *, #116509, .T. ) ;
#5106=AXIS2_PLACEMENT_3D ( 'NONE', #28098, #30230, #18614 ) ;
#5107=DIRECTION ( 'NONE',  ( 0.7071067811865487940, 0.7071067811865463515, 0.000000000000000000 ) ) ;
#5108=VECTOR ( 'NONE', #105783, 1000.000000000000000 ) ;
#5109=AXIS2_PLACEMENT_3D ( 'NONE', #47096, #124590, #108503 ) ;
#5110=CARTESIAN_POINT ( 'NONE',  ( 14.51078643762690490, -27.52281430457045275, 5.000000000000000000 ) ) ;
#5111=CARTESIAN_POINT ( 'NONE',  ( 21.18398860626899349, 28.73617430169802134, 5.000000000000000000 ) ) ;
#5112=EDGE_LOOP ( 'NONE', ( #125094, #75208, #103008, #52872 ) ) ;
#5113=CARTESIAN_POINT ( 'NONE',  ( -13.08316395874281568, 3.014287036135060660, 4.000000000000000000 ) ) ;
#5115=DIRECTION ( 'NONE',  ( 0.6830127018922181881, 0.6830127018922202975, -0.2588190451025214056 ) ) ;
#5116=ORIENTED_EDGE ( 'NONE', *, *, #30766, .T. ) ;
#5118=PLANE ( 'NONE',  #6944 ) ;
#5119=ORIENTED_EDGE ( 'NONE', *, *, #142151, .F. ) ;
#5120=ADVANCED_FACE ( 'NONE', ( #36319 ), #48617, .F. ) ;
#5121=VERTEX_POINT ( 'NONE', #81997 ) ;
#5122=CARTESIAN_POINT ( 'NONE',  ( -27.18398860626900060, 28.73617430169806042, 5.000000000000000000 ) ) ;
#5123=CARTESIAN_POINT ( 'NONE',  ( -16.49999999999987566, -2.947814304570798960, 5.000000000000000000 ) ) ;
#5125=ORIENTED_EDGE ( 'NONE', *, *, #126744, .F. ) ;
#5126=DIRECTION ( 'NONE',  ( -0.000000000000000000, 0.3543493200069152138, -0.9351131265310292928 ) ) ;
#5127=CARTESIAN_POINT ( 'NONE',  ( -23.99999999999982947, -21.41253812416053748, 4.000000000000000000 ) ) ;
#5128=LINE ( 'NONE', #5850, #103938 ) ;
#5129=ORIENTED_EDGE ( 'NONE', *, *, #84871, .T. ) ;
#5132=CARTESIAN_POINT ( 'NONE',  ( 26.70025512860841488, -27.71228299555187391, 4.000000000000000000 ) ) ;
#5133=CARTESIAN_POINT ( 'NONE',  ( -6.792893218813407685, -17.24070752338409918, 5.000000000000000000 ) ) ;
#5134=LINE ( 'NONE', #28368, #400 ) ;
#5135=VECTOR ( 'NONE', #21472, 1000.000000000000000 ) ;
#5137=DIRECTION ( 'NONE',  ( -0.6830127018922181881, 0.6830127018922202975, -0.2588190451025214056 ) ) ;
#5138=VECTOR ( 'NONE', #89169, 1000.000000000000000 ) ;
#5139=DIRECTION ( 'NONE',  ( 0.6830127018922181881, 0.6830127018922202975, -0.2588190451025214056 ) ) ;
#5140=CARTESIAN_POINT ( 'NONE',  ( 56.99451991528749062, 28.92564299267978001, 4.000000000000000000 ) ) ;
#5142=ORIENTED_EDGE ( 'NONE', *, *, #104313, .T. ) ;
#5144=ORIENTED_EDGE ( 'NONE', *, *, #23139, .T. ) ;
#5145=VERTEX_POINT ( 'NONE', #60970 ) ;
#5147=ORIENTED_EDGE ( 'NONE', *, *, #141225, .F. ) ;
#5149=ORIENTED_EDGE ( 'NONE', *, *, #29661, .T. ) ;
#5150=AXIS2_PLACEMENT_3D ( 'NONE', #129062, #76125, #42804 ) ;
#5151=CARTESIAN_POINT ( 'NONE',  ( 2.999999999999976907, -21.03360074219752462, 5.000000000000000000 ) ) ;
#5152=CARTESIAN_POINT ( 'NONE',  ( -27.48921356237309155, -27.52281430457074762, 5.000000000000000000 ) ) ;
#5153=EDGE_CURVE ( 'NONE', #69796, #12358, #105130, .T. ) ;
#5155=EDGE_CURVE ( 'NONE', #12589, #93689, #8620, .T. ) ;
#5156=ORIENTED_EDGE ( 'NONE', *, *, #65784, .T. ) ;
#5161=EDGE_LOOP ( 'NONE', ( #133934, #96863, #25673, #79675 ) ) ;
#5162=CARTESIAN_POINT ( 'NONE',  ( 54.48921356237310221, -27.52281430457093236, 5.000000000000000000 ) ) ;
#5166=PLANE ( 'NONE',  #128497 ) ;
#5167=LINE ( 'NONE', #16036, #30677 ) ;
#5168=CARTESIAN_POINT ( 'NONE',  ( 60.18398860626900415, 28.73617430169829490, 5.000000000000000000 ) ) ;
#5170=LINE ( 'NONE', #107370, #137004 ) ;
#5171=CARTESIAN_POINT ( 'NONE',  ( -14.99999999999990230, 8.587461875839165870, 4.000000000000000000 ) ) ;
#5172=ORIENTED_EDGE ( 'NONE', *, *, #88595, .F. ) ;
#5176=VERTEX_POINT ( 'NONE', #9340 ) ;
#5177=FACE_OUTER_BOUND ( 'NONE', #82518, .T. ) ;
#5178=EDGE_CURVE ( 'NONE', #1349, #124601, #118858, .T. ) ;
#5179=LINE ( 'NONE', #117518, #108024 ) ;
#5180=ORIENTED_EDGE ( 'NONE', *, *, #57135, .F. ) ;
#5181=VECTOR ( 'NONE', #111797, 1000.000000000000000 ) ;
#5183=VECTOR ( 'NONE', #64820, 1000.000000000000000 ) ;
#5184=DIRECTION ( 'NONE',  ( 1.000000000000000000, 0.000000000000000000, 0.000000000000000000 ) ) ;
#5185=DIRECTION ( 'NONE',  ( -0.000000000000000000, 0.3543493200069153248, 0.9351131265310292928 ) ) ;
#5186=ADVANCED_FACE ( 'NONE', ( #84130 ), #84809, .F. ) ;
#5187=AXIS2_PLACEMENT_3D ( 'NONE', #143136, #88047, #132299 ) ;
#5188=ADVANCED_FACE ( 'NONE', ( #128332 ), #75373, .F. ) ;
#5191=VECTOR ( 'NONE', #9327, 1000.000000000000000 ) ;
#5195=CARTESIAN_POINT ( 'NONE',  ( 7.828169399223478209, 18.75929247661553134, 4.000000000000000000 ) ) ;
#5197=VECTOR ( 'NONE', #36566, 999.9999999999998863 ) ;
#5199=PLANE ( 'NONE',  #96088 ) ;
#5200=ADVANCED_FACE ( 'NONE', ( #50758 ), #31163, .F. ) ;
#5202=CARTESIAN_POINT ( 'NONE',  ( -25.49999999999982236, -6.839392718269155402, -8.480912228396030983 ) ) ;
#5203=FACE_OUTER_BOUND ( 'NONE', #73505, .T. ) ;
#5204=EDGE_LOOP ( 'NONE', ( #126905, #63380, #79758, #78840 ) ) ;
#5208=DIRECTION ( 'NONE',  ( 0.6830127018922180770, -0.6830127018922204085, -0.2588190451025213501 ) ) ;
#5209=ADVANCED_FACE ( 'NONE', ( #139217 ), #117406, .T. ) ;
#5210=DIRECTION ( 'NONE',  ( -0.7071067811865486830, -0.7071067811865464625, -0.000000000000000000 ) ) ;
#5211=LINE ( 'NONE', #70548, #142688 ) ;
#5212=CARTESIAN_POINT ( 'NONE',  ( 3.005480084712505828, 28.92564299267936079, 4.000000000000000000 ) ) ;
#5213=EDGE_CURVE ( 'NONE', #136929, #78067, #30436, .T. ) ;
#5214=VECTOR ( 'NONE', #12643, 999.9999999999998863 ) ;
#5215=EDGE_CURVE ( 'NONE', #98856, #139660, #53624, .T. ) ;
#5217=EDGE_LOOP ( 'NONE', ( #1220, #58444, #7138, #128696 ) ) ;
#5218=FACE_OUTER_BOUND ( 'NONE', #103278, .T. ) ;
#5219=CARTESIAN_POINT ( 'NONE',  ( 32.67183060077624646, 8.259292476615641476, 4.000000000000000000 ) ) ;
#5220=VERTEX_POINT ( 'NONE', #142071 ) ;
#5221=EDGE_LOOP ( 'NONE', ( #19398, #116849, #39864, #109067 ) ) ;
#5222=CARTESIAN_POINT ( 'NONE',  ( 27.18398860626900060, 28.73617430169806042, 5.000000000000000000 ) ) ;
#5223=EDGE_CURVE ( 'NONE', #141807, #10669, #51480, .T. ) ;
#5224=EDGE_LOOP ( 'NONE', ( #140424, #133525, #137951, #17815 ) ) ;
#5229=VECTOR ( 'NONE', #89646, 1000.000000000000000 ) ;
#5230=LINE ( 'NONE', #62511, #25199 ) ;
#5232=EDGE_CURVE ( 'NONE', #14025, #122052, #42038, .T. ) ;
#5233=LINE ( 'NONE', #69845, #249 ) ;
#5234=FACE_BOUND ( 'NONE', #17612, .T. ) ;
#5236=LINE ( 'NONE', #93707, #57273 ) ;
#5237=EDGE_LOOP ( 'NONE', ( #98325, #60848, #131880, #72364 ) ) ;
#5239=FACE_OUTER_BOUND ( 'NONE', #99203, .T. ) ;
#5241=EDGE_CURVE ( 'NONE', #40729, #118475, #6477, .T. ) ;
#5242=DIRECTION ( 'NONE',  ( -0.3543493200069162685, -0.000000000000000000, -0.9351131265310288487 ) ) ;
#5243=ORIENTED_EDGE ( 'NONE', *, *, #76814, .F. ) ;
#5244=EDGE_CURVE ( 'NONE', #4593, #84994, #73935, .T. ) ;
#5245=EDGE_CURVE ( 'NONE', #45336, #104888, #63088, .T. ) ;
#5246=ORIENTED_EDGE ( 'NONE', *, *, #129800, .T. ) ;
#5248=ORIENTED_EDGE ( 'NONE', *, *, #43692, .F. ) ;
#5250=CARTESIAN_POINT ( 'NONE',  ( -29.99999999999978684, -7.068876922607743474, 4.000000000000000000 ) ) ;
#5251=DIRECTION ( 'NONE',  ( -0.6830127018922181881, 0.6830127018922202975, -0.2588190451025214056 ) ) ;
#5252=VECTOR ( 'NONE', #127963, 1000.000000000000000 ) ;
#5253=ORIENTED_EDGE ( 'NONE', *, *, #6302, .T. ) ;
#5254=FACE_OUTER_BOUND ( 'NONE', #125304, .T. ) ;
#5255=AXIS2_PLACEMENT_3D ( 'NONE', #136596, #113414, #80822 ) ;
#5256=ADVANCED_FACE ( 'NONE', ( #110109 ), #78962, .F. ) ;
#5257=CARTESIAN_POINT ( 'NONE',  ( -34.92500000000001137, -22.22500000000000142, 4.000000000000000000 ) ) ;
#5258=CARTESIAN_POINT ( 'NONE',  ( -37.26506670282027045, 12.75929247661558996, 18.34774599283964847 ) ) ;
#5259=CARTESIAN_POINT ( 'NONE',  ( -14.20666063542142687, 21.75929247661549937, 4.998822639870708073 ) ) ;
#5260=FACE_OUTER_BOUND ( 'NONE', #51654, .T. ) ;
#5261=ORIENTED_EDGE ( 'NONE', *, *, #138909, .T. ) ;
#5262=AXIS2_PLACEMENT_3D ( 'NONE', #51972, #115742, #60744 ) ;
#5263=ORIENTED_EDGE ( 'NONE', *, *, #130098, .T. ) ;
#5265=LINE ( 'NONE', #38642, #120684 ) ;
#5266=ORIENTED_EDGE ( 'NONE', *, *, #48611, .T. ) ;
#5268=VERTEX_POINT ( 'NONE', #123169 ) ;
#5269=CARTESIAN_POINT ( 'NONE',  ( 0.4892135623730947680, -27.52281430457055578, 5.000000000000000000 ) ) ;
#5270=DIRECTION ( 'NONE',  ( 2.781805975412905274E-17, -0.3543493200069152138, 0.9351131265310292928 ) ) ;
#5271=VECTOR ( 'NONE', #123975, 1000.000000000000227 ) ;
#5272=ORIENTED_EDGE ( 'NONE', *, *, #3330, .T. ) ;
#5273=LINE ( 'NONE', #16897, #113426 ) ;
#5274=DIRECTION ( 'NONE',  ( -0.7071067811865486830, -0.7071067811865464625, 0.000000000000000000 ) ) ;
#5276=CARTESIAN_POINT ( 'NONE',  ( 31.49999999999977973, -12.66682484999663494, -0.6294897503863212673 ) ) ;
#5278=CARTESIAN_POINT ( 'NONE',  ( 6.793339364578431017, 21.75929247661549226, 4.998822639870705409 ) ) ;
#5279=LINE ( 'NONE', #139431, #55867 ) ;
#5280=ADVANCED_FACE ( 'NONE', ( #34016 ), #134774, .F. ) ;
#5282=CYLINDRICAL_SURFACE ( 'NONE', #140120, 0.5000000000000004441 ) ;
#5283=VECTOR ( 'NONE', #19595, 1000.000000000000000 ) ;
#5284=CARTESIAN_POINT ( 'NONE',  ( 7.499999999999951150, 10.94296225409028089, -9.576120664313240383 ) ) ;
#5285=ORIENTED_EDGE ( 'NONE', *, *, #68839, .F. ) ;
#5286=LINE ( 'NONE', #84336, #12351 ) ;
#5287=ORIENTED_EDGE ( 'NONE', *, *, #120968, .F. ) ;
#5288=PLANE ( 'NONE',  #68133 ) ;
#5290=AXIS2_PLACEMENT_3D ( 'NONE', #95168, #62568, #51695 ) ;
#5291=CARTESIAN_POINT ( 'NONE',  ( 27.48921356237309155, -27.52281430457074762, 5.000000000000000000 ) ) ;
#5292=AXIS2_PLACEMENT_3D ( 'NONE', #258, #44555, #131524 ) ;
#5293=ORIENTED_EDGE ( 'NONE', *, *, #53400, .T. ) ;
#5294=EDGE_CURVE ( 'NONE', #126528, #122084, #35464, .T. ) ;
#5295=DIRECTION ( 'NONE',  ( 0.7071067811865487940, 0.7071067811865463515, -0.000000000000000000 ) ) ;
#5296=PLANE ( 'NONE',  #46575 ) ;
#5297=DIRECTION ( 'NONE',  ( -0.7071067811865486830, -0.7071067811865464625, 0.000000000000000000 ) ) ;
#5298=VECTOR ( 'NONE', #129944, 1000.000000000000000 ) ;
#5299=VECTOR ( 'NONE', #87578, 1000.000000000000000 ) ;
#5300=ORIENTED_EDGE ( 'NONE', *, *, #13481, .F. ) ;
#5301=LINE ( 'NONE', #126381, #13485 ) ;
#5304=EDGE_CURVE ( 'NONE', #17012, #28108, #23081, .T. ) ;
#5305=PLANE ( 'NONE',  #5435 ) ;
#5307=EDGE_CURVE ( 'NONE', #126328, #8088, #134036, .T. ) ;
#5308=VERTEX_POINT ( 'NONE', #131891 ) ;
#5309=ORIENTED_EDGE ( 'NONE', *, *, #83609, .F. ) ;
#5310=CYLINDRICAL_SURFACE ( 'NONE', #881, 0.5000000000000004441 ) ;
#5311=DIRECTION ( 'NONE',  ( 0.3543493200069162685, -0.000000000000000000, -0.9351131265310288487 ) ) ;
#5312=EDGE_CURVE ( 'NONE', #21371, #99152, #54360, .T. ) ;
#5313=ADVANCED_FACE ( 'NONE', ( #111553 ), #23841, .F. ) ;
#5316=DIRECTION ( 'NONE',  ( 0.7071067811865487940, 0.7071067811865463515, 0.000000000000000000 ) ) ;
#5317=VECTOR ( 'NONE', #8169, 1000.000000000000000 ) ;
#5318=CARTESIAN_POINT ( 'NONE',  ( 36.18398860626899705, 28.73617430169812437, 5.000000000000000000 ) ) ;
#5319=CARTESIAN_POINT ( 'NONE',  ( 21.48921356237309155, -27.52281430457070499, 5.000000000000000000 ) ) ;
#5320=PLANE ( 'NONE',  #102304 ) ;
#5321=ORIENTED_EDGE ( 'NONE', *, *, #78197, .T. ) ;
#5322=EDGE_CURVE ( 'NONE', #98347, #86060, #87665, .T. ) ;
#5323=CARTESIAN_POINT ( 'NONE',  ( 21.48921356237309155, -27.52281430457070499, 5.000000000000000000 ) ) ;
#5324=LINE ( 'NONE', #135867, #127994 ) ;
#5328=FACE_OUTER_BOUND ( 'NONE', #12416, .T. ) ;
#5329=EDGE_CURVE ( 'NONE', #14772, #69972, #77534, .T. ) ;
#5330=ORIENTED_EDGE ( 'NONE', *, *, #30443, .F. ) ;
#5331=CARTESIAN_POINT ( 'NONE',  ( 0.000000000000000000, -21.72500000000000142, 4.500000000000000888 ) ) ;
#5333=ORIENTED_EDGE ( 'NONE', *, *, #83842, .T. ) ;
#5334=ORIENTED_EDGE ( 'NONE', *, *, #99976, .T. ) ;
#5335=LINE ( 'NONE', #116967, #89439 ) ;
#5337=DIRECTION ( 'NONE',  ( -0.6830127018922181881, 0.6830127018922202975, -0.2588190451025214056 ) ) ;
#5338=DIRECTION ( 'NONE',  ( 0.7071067811865487940, 0.7071067811865463515, -0.000000000000000000 ) ) ;
#5339=CARTESIAN_POINT ( 'NONE',  ( 69.29974487139159578, -27.71228299555254537, 4.000000000000000000 ) ) ;
#5342=CARTESIAN_POINT ( 'NONE',  ( 8.673617379884035472E-16, -18.41253812416056945, 4.000000000000000000 ) ) ;
#5343=CARTESIAN_POINT ( 'NONE',  ( -39.29974487139159578, -27.71228299555233576, 4.000000000000000000 ) ) ;
#5344=ADVANCED_FACE ( 'NONE', ( #55771 ), #110808, .T. ) ;
#5345=CARTESIAN_POINT ( 'NONE',  ( 34.42499999999998295, -21.72500000000000142, 4.500000000000000888 ) ) ;
#5346=PLANE ( 'NONE',  #28838 ) ;
#5347=DIRECTION ( 'NONE',  ( -0.6830127018922181881, 0.6830127018922202975, -0.2588190451025214056 ) ) ;
#5348=VECTOR ( 'NONE', #12289, 1000.000000000000000 ) ;
#5352=ORIENTED_EDGE ( 'NONE', *, *, #102088, .F. ) ;
#5353=VERTEX_POINT ( 'NONE', #115793 ) ;
#5355=DIRECTION ( 'NONE',  ( -0.000000000000000000, -0.3543493200069152693, 0.9351131265310292928 ) ) ;
#5356=LINE ( 'NONE', #6054, #92491 ) ;
#5357=CARTESIAN_POINT ( 'NONE',  ( -34.92500000000001137, 22.22500000000000142, 4.000000000000000000 ) ) ;
#5360=ORIENTED_EDGE ( 'NONE', *, *, #9632, .T. ) ;
#5361=DIRECTION ( 'NONE',  ( 0.6830127018922181881, 0.6830127018922202975, -0.2588190451025214056 ) ) ;
#5362=EDGE_CURVE ( 'NONE', #35109, #85516, #136875, .T. ) ;
#5363=LINE ( 'NONE', #138051, #113851 ) ;
#5365=EDGE_CURVE ( 'NONE', #64063, #79833, #57041, .T. ) ;
#5366=DIRECTION ( 'NONE',  ( -0.7071067811865486830, -0.7071067811865464625, 0.000000000000000000 ) ) ;
#5367=ORIENTED_EDGE ( 'NONE', *, *, #88840, .T. ) ;
#5368=VERTEX_POINT ( 'NONE', #1855 ) ;
#5369=AXIS2_PLACEMENT_3D ( 'NONE', #26537, #81661, #90356 ) ;
#5370=CARTESIAN_POINT ( 'NONE',  ( -0.1839886062690032631, 28.73617430169787568, 5.000000000000000000 ) ) ;
#5372=DIRECTION ( 'NONE',  ( 1.000000000000000000, 0.000000000000000000, 0.000000000000000000 ) ) ;
#5374=CARTESIAN_POINT ( 'NONE',  ( -3.005480084712505828, 28.92564299267936079, 4.000000000000000000 ) ) ;
#5375=CARTESIAN_POINT ( 'NONE',  ( 0.000000000000000000, 0.000000000000000000, 5.000000000000000000 ) ) ;
#5376=ORIENTED_EDGE ( 'NONE', *, *, #121412, .F. ) ;
#5377=CARTESIAN_POINT ( 'NONE',  ( 11.99999999999992717, 14.96639925780211478, 5.000000000000000000 ) ) ;
#5378=DIRECTION ( 'NONE',  ( -0.7071067811865486830, 0.7071067811865464625, 0.000000000000000000 ) ) ;
#5380=CARTESIAN_POINT ( 'NONE',  ( -24.52400138585431222, 22.03583458319438293, 4.979811245910084949 ) ) ;
#5381=CARTESIAN_POINT ( 'NONE',  ( 26.20710678118635784, -8.240707523384202204, 5.000000000000000000 ) ) ;
#5384=EDGE_CURVE ( 'NONE', #90006, #100364, #111366, .T. ) ;
#5385=LINE ( 'NONE', #94541, #17430 ) ;
#5386=LINE ( 'NONE', #103280, #67329 ) ;
#5388=CARTESIAN_POINT ( 'NONE',  ( -34.49999999999975842, 15.05432934483078533, 4.994342998332167660 ) ) ;
#5389=ORIENTED_EDGE ( 'NONE', *, *, #65968, .T. ) ;
#5391=AXIS2_PLACEMENT_3D ( 'NONE', #62238, #106393, #117284 ) ;
#5392=DIRECTION ( 'NONE',  ( -0.000000000000000000, 0.000000000000000000, 1.000000000000000000 ) ) ;
#5393=CARTESIAN_POINT ( 'NONE',  ( -34.47516574401890210, 9.028067341115725952, 4.998110765256836174 ) ) ;
#5394=EDGE_CURVE ( 'NONE', #12987, #23088, #132470, .T. ) ;
#5395=ORIENTED_EDGE ( 'NONE', *, *, #141871, .F. ) ;
#5397=ORIENTED_EDGE ( 'NONE', *, *, #116605, .F. ) ;
#5398=DIRECTION ( 'NONE',  ( -0.000000000000000000, -0.3543493200069152693, 0.9351131265310292928 ) ) ;
#5399=ORIENTED_EDGE ( 'NONE', *, *, #19090, .T. ) ;
#5400=DIRECTION ( 'NONE',  ( 0.000000000000000000, 0.000000000000000000, 1.000000000000000000 ) ) ;
#5401=VECTOR ( 'NONE', #119669, 1000.000000000000000 ) ;
#5402=ORIENTED_EDGE ( 'NONE', *, *, #123377, .T. ) ;
#5403=FACE_BOUND ( 'NONE', #109297, .T. ) ;
#5405=LINE ( 'NONE', #48959, #28089 ) ;
#5406=CARTESIAN_POINT ( 'NONE',  ( 51.48921356237309510, -27.52281430457091460, 5.000000000000000000 ) ) ;
#5407=DIRECTION ( 'NONE',  ( 1.000000000000000000, 0.000000000000000000, 0.000000000000000000 ) ) ;
#5408=VERTEX_POINT ( 'NONE', #69324 ) ;
#5409=VECTOR ( 'NONE', #52334, 1000.000000000000227 ) ;
#5413=EDGE_CURVE ( 'NONE', #117635, #74571, #37397, .T. ) ;
#5414=VECTOR ( 'NONE', #71002, 1000.000000000000000 ) ;
#5415=ORIENTED_EDGE ( 'NONE', *, *, #101835, .T. ) ;
#5417=ORIENTED_EDGE ( 'NONE', *, *, #110926, .T. ) ;
#5418=LINE ( 'NONE', #61312, #48935 ) ;
#5419=CARTESIAN_POINT ( 'NONE',  ( 34.82816939922328459, -20.24070752338408141, 4.000000000000000000 ) ) ;
#5420=EDGE_CURVE ( 'NONE', #120324, #135031, #103338, .T. ) ;
#5421=VECTOR ( 'NONE', #136523, 1000.000000000000000 ) ;
#5422=DIRECTION ( 'NONE',  ( 1.000000000000000000, 0.000000000000000000, 0.000000000000000000 ) ) ;
#5423=ORIENTED_EDGE ( 'NONE', *, *, #3650, .T. ) ;
#5424=PLANE ( 'NONE',  #106200 ) ;
#5426=VECTOR ( 'NONE', #133011, 1000.000000000000000 ) ;
#5427=LINE ( 'NONE', #51118, #1760 ) ;
#5429=CARTESIAN_POINT ( 'NONE',  ( -0.1839886062690032631, 28.73617430169787568, 5.000000000000000000 ) ) ;
#5430=LINE ( 'NONE', #52522, #127340 ) ;
#5431=LINE ( 'NONE', #38810, #28343 ) ;
#5432=ORIENTED_EDGE ( 'NONE', *, *, #91890, .F. ) ;
#5433=LINE ( 'NONE', #114219, #126007 ) ;
#5434=DIRECTION ( 'NONE',  ( -0.000000000000000000, -0.3543493200069153248, 0.9351131265310292928 ) ) ;
#5435=AXIS2_PLACEMENT_3D ( 'NONE', #82214, #15448, #71318 ) ;
#5436=ORIENTED_EDGE ( 'NONE', *, *, #113123, .F. ) ;
#5437=ORIENTED_EDGE ( 'NONE', *, *, #73607, .T. ) ;
#5438=ORIENTED_EDGE ( 'NONE', *, *, #124996, .F. ) ;
#5440=ORIENTED_EDGE ( 'NONE', *, *, #116761, .T. ) ;
#5441=VECTOR ( 'NONE', #118484, 1000.000000000000227 ) ;
#5442=AXIS2_PLACEMENT_3D ( 'NONE', #129028, #128344, #18091 ) ;
#5445=ORIENTED_EDGE ( 'NONE', *, *, #100350, .F. ) ;
#5447=ORIENTED_EDGE ( 'NONE', *, *, #93, .F. ) ;
#5448=CARTESIAN_POINT ( 'NONE',  ( 51.48921356237309510, -27.52281430457091460, 5.000000000000000000 ) ) ;
#5450=CARTESIAN_POINT ( 'NONE',  ( -33.32816939922329880, 8.259292476615641476, 4.000000000000000000 ) ) ;
#5451=CARTESIAN_POINT ( 'NONE',  ( -14.99451991528749595, 28.92564299267948513, 4.000000000000000000 ) ) ;
#5452=ORIENTED_EDGE ( 'NONE', *, *, #11165, .T. ) ;
#5453=ORIENTED_EDGE ( 'NONE', *, *, #7910, .T. ) ;
#5454=DIRECTION ( 'NONE',  ( -0.000000000000000000, 0.000000000000000000, 1.000000000000000000 ) ) ;
#5455=LINE ( 'NONE', #141538, #71628 ) ;
#5456=ORIENTED_EDGE ( 'NONE', *, *, #89348, .F. ) ;
#5457=LINE ( 'NONE', #28691, #4037 ) ;
#5458=ADVANCED_FACE ( 'NONE', ( #101935 ), #70764, .F. ) ;
#5459=ORIENTED_EDGE ( 'NONE', *, *, #79236, .T. ) ;
#5460=ORIENTED_EDGE ( 'NONE', *, *, #128680, .F. ) ;
#5461=ORIENTED_EDGE ( 'NONE', *, *, #35306, .T. ) ;
#5462=ORIENTED_EDGE ( 'NONE', *, *, #111476, .F. ) ;
#5463=EDGE_CURVE ( 'NONE', #139982, #133491, #38122, .T. ) ;
#5465=LINE ( 'NONE', #138160, #93462 ) ;
#5466=VECTOR ( 'NONE', #110488, 1000.000000000000227 ) ;
#5467=CARTESIAN_POINT ( 'NONE',  ( -11.99999999999990763, 2.966399257802230682, 5.000000000000000000 ) ) ;
#5468=FACE_OUTER_BOUND ( 'NONE', #120833, .T. ) ;
#5469=FACE_OUTER_BOUND ( 'NONE', #115963, .T. ) ;
#5470=ADVANCED_FACE ( 'NONE', ( #114910 ), #14201, .F. ) ;
#5471=ADVANCED_FACE ( 'NONE', ( #25794 ), #125847, .F. ) ;
#5473=VECTOR ( 'NONE', #140210, 1000.000000000000000 ) ;
#5474=EDGE_LOOP ( 'NONE', ( #54486, #31306, #40166, #48365 ) ) ;
#5475=LINE ( 'NONE', #27238, #49391 ) ;
#5476=EDGE_CURVE ( 'NONE', #132130, #27153, #26520, .T. ) ;
#5477=EDGE_CURVE ( 'NONE', #60182, #20317, #59868, .T. ) ;
#5478=FACE_OUTER_BOUND ( 'NONE', #11652, .T. ) ;
#5480=AXIS2_PLACEMENT_3D ( 'NONE', #116551, #60048, #62914 ) ;
#5482=LINE ( 'NONE', #83078, #58259 ) ;
#5483=VERTEX_POINT ( 'NONE', #80909 ) ;
#5484=ORIENTED_EDGE ( 'NONE', *, *, #140971, .T. ) ;
#5486=ORIENTED_EDGE ( 'NONE', *, *, #71263, .F. ) ;
#5488=DIRECTION ( 'NONE',  ( 0.7071067811865487940, 0.7071067811865463515, 0.000000000000000000 ) ) ;
#5491=EDGE_CURVE ( 'NONE', #106060, #18279, #48997, .T. ) ;
#5492=CARTESIAN_POINT ( 'NONE',  ( 4.828169399223495084, -17.24070752338410628, 4.000000000000000000 ) ) ;
#5495=VECTOR ( 'NONE', #4123, 1000.000000000000000 ) ;
#5497=EDGE_CURVE ( 'NONE', #80916, #4279, #114236, .T. ) ;
#5498=LINE ( 'NONE', #128043, #66961 ) ;
#5499=CARTESIAN_POINT ( 'NONE',  ( -29.99451991528749417, 28.92564299267958816, 4.000000000000000000 ) ) ;
#5501=DIRECTION ( 'NONE',  ( 0.7071067811865487940, -0.7071067811865463515, 0.000000000000000000 ) ) ;
#5502=EDGE_LOOP ( 'NONE', ( #116858, #88069, #38211, #87346 ) ) ;
#5503=DIRECTION ( 'NONE',  ( 0.7071067811865487940, 0.7071067811865463515, -0.000000000000000000 ) ) ;
#5505=EDGE_CURVE ( 'NONE', #122142, #2143, #47601, .T. ) ;
#5506=PLANE ( 'NONE',  #110790 ) ;
#5507=CARTESIAN_POINT ( 'NONE',  ( 9.489213562373095101, -27.52281430457062328, 5.000000000000000000 ) ) ;
#5508=ORIENTED_EDGE ( 'NONE', *, *, #25375, .F. ) ;
#5509=CARTESIAN_POINT ( 'NONE',  ( 23.99999999999983302, -16.60178936734445898, 0.8616154019348044590 ) ) ;
#5510=LINE ( 'NONE', #26576, #121275 ) ;
#5511=EDGE_LOOP ( 'NONE', ( #41415, #26073, #108408, #135094 ) ) ;
#5514=ORIENTED_EDGE ( 'NONE', *, *, #129310, .F. ) ;
#5515=VECTOR ( 'NONE', #30976, 1000.000000000000000 ) ;
#5516=ADVANCED_FACE ( 'NONE', ( #93196 ), #46909, .F. ) ;
#5517=LINE ( 'NONE', #49794, #140193 ) ;
#5520=VECTOR ( 'NONE', #122302, 1000.000000000000227 ) ;
#5522=VERTEX_POINT ( 'NONE', #79529 ) ;
#5523=LINE ( 'NONE', #124472, #125651 ) ;
#5524=CARTESIAN_POINT ( 'NONE',  ( -10.49999999999992539, 15.05218569542901896, 5.000000000000000000 ) ) ;
#5526=EDGE_CURVE ( 'NONE', #8455, #69699, #68623, .T. ) ;
#5527=DIRECTION ( 'NONE',  ( -0.7071067811865486830, 0.7071067811865464625, 0.000000000000000000 ) ) ;
#5529=ORIENTED_EDGE ( 'NONE', *, *, #116995, .T. ) ;
#5530=VECTOR ( 'NONE', #85008, 1000.000000000000000 ) ;
#5531=CARTESIAN_POINT ( 'NONE',  ( -17.99999999999986855, 12.25461709320619086, -10.07315571508701346 ) ) ;
#5532=EDGE_CURVE ( 'NONE', #94185, #68343, #112805, .T. ) ;
#5533=VERTEX_POINT ( 'NONE', #35991 ) ;
#5534=VECTOR ( 'NONE', #85717, 1000.000000000000227 ) ;
#5538=DIRECTION ( 'NONE',  ( 0.7071067811865487940, 0.7071067811865463515, 0.000000000000000000 ) ) ;
#5539=DIRECTION ( 'NONE',  ( -0.7071067811865486830, -0.7071067811865464625, 0.000000000000000000 ) ) ;
#5540=DIRECTION ( 'NONE',  ( 1.000000000000000000, 0.000000000000000000, 0.000000000000000000 ) ) ;
#5541=VERTEX_POINT ( 'NONE', #97258 ) ;
#5543=ADVANCED_FACE ( 'NONE', ( #30641 ), #108143, .T. ) ;
#5544=VECTOR ( 'NONE', #63325, 1000.000000000000227 ) ;
#5545=ADVANCED_FACE ( 'NONE', ( #66123 ), #109599, .F. ) ;
#5546=LINE ( 'NONE', #116474, #78951 ) ;
#5547=LINE ( 'NONE', #71555, #25414 ) ;
#5550=ORIENTED_EDGE ( 'NONE', *, *, #116830, .F. ) ;
#5552=DIRECTION ( 'NONE',  ( -0.7071067811865486830, -0.7071067811865464625, 0.000000000000000000 ) ) ;
#5555=AXIS2_PLACEMENT_3D ( 'NONE', #129014, #114040, #92269 ) ;
#5556=ORIENTED_EDGE ( 'NONE', *, *, #90587, .T. ) ;
#5557=ORIENTED_EDGE ( 'NONE', *, *, #107950, .T. ) ;
#5558=EDGE_LOOP ( 'NONE', ( #100792, #1255, #52559, #139846 ) ) ;
#5560=VECTOR ( 'NONE', #9753, 999.9999999999998863 ) ;
#5561=ORIENTED_EDGE ( 'NONE', *, *, #88034, .F. ) ;
#5562=EDGE_CURVE ( 'NONE', #7059, #2171, #32786, .T. ) ;
#5563=LINE ( 'NONE', #83152, #107669 ) ;
#5564=DIRECTION ( 'NONE',  ( -0.000000000000000000, -0.3543493200069152693, 0.9351131265310292928 ) ) ;
#5565=VECTOR ( 'NONE', #25127, 1000.000000000000227 ) ;
#5566=LINE ( 'NONE', #102777, #82797 ) ;
#5567=LINE ( 'NONE', #49838, #59495 ) ;
#5568=ORIENTED_EDGE ( 'NONE', *, *, #11403, .T. ) ;
#5569=DIRECTION ( 'NONE',  ( 0.3543493200069162685, -0.000000000000000000, -0.9351131265310288487 ) ) ;
#5570=DIRECTION ( 'NONE',  ( 0.7071067811865487940, 0.7071067811865463515, 0.000000000000000000 ) ) ;
#5571=ORIENTED_EDGE ( 'NONE', *, *, #24484, .T. ) ;
#5572=ADVANCED_FACE ( 'NONE', ( #43629 ), #86445, .F. ) ;
#5575=VECTOR ( 'NONE', #24576, 1000.000000000000000 ) ;
#5576=CARTESIAN_POINT ( 'NONE',  ( -20.51078643762690490, -27.52281430457041012, 5.000000000000000000 ) ) ;
#5577=ORIENTED_EDGE ( 'NONE', *, *, #20914, .F. ) ;
#5578=ORIENTED_EDGE ( 'NONE', *, *, #35599, .T. ) ;
#5579=EDGE_CURVE ( 'NONE', #19199, #98041, #42943, .T. ) ;
#5580=DIRECTION ( 'NONE',  ( -0.6830127018922181881, 0.6830127018922202975, -0.2588190451025214056 ) ) ;
#5581=LINE ( 'NONE', #83920, #52404 ) ;
#5583=DIRECTION ( 'NONE',  ( -0.7071067811865487940, 0.7071067811865463515, -0.000000000000000000 ) ) ;
#5584=DIRECTION ( 'NONE',  ( -0.7071067811865486830, -0.7071067811865464625, -0.000000000000000000 ) ) ;
#5585=DIRECTION ( 'NONE',  ( -0.7071067811865486830, -0.7071067811865464625, 0.000000000000000000 ) ) ;
#5586=LINE ( 'NONE', #70213, #51246 ) ;
#5587=ORIENTED_EDGE ( 'NONE', *, *, #119608, .F. ) ;
#5588=VERTEX_POINT ( 'NONE', #53064 ) ;
#5589=EDGE_LOOP ( 'NONE', ( #100201, #128538, #8060, #46993 ) ) ;
#5590=ORIENTED_EDGE ( 'NONE', *, *, #63831, .F. ) ;
#5591=VECTOR ( 'NONE', #435, 999.9999999999998863 ) ;
#5592=ADVANCED_FACE ( 'NONE', ( #53822 ), #85693, .F. ) ;
#5593=CARTESIAN_POINT ( 'NONE',  ( -14.99999999999989519, 9.631307414974306980, -9.079085613539573885 ) ) ;
#5596=ORIENTED_EDGE ( 'NONE', *, *, #140747, .F. ) ;
#5598=DIRECTION ( 'NONE',  ( 0.6830127018922181881, 0.6830127018922202975, -0.2588190451025214056 ) ) ;
#5599=PLANE ( 'NONE',  #87807 ) ;
#5600=DIRECTION ( 'NONE',  ( 0.3543493200069163240, -0.000000000000000000, -0.9351131265310288487 ) ) ;
#5601=ORIENTED_EDGE ( 'NONE', *, *, #24105, .F. ) ;
#5602=CARTESIAN_POINT ( 'NONE',  ( 18.10180811604841011, 9.068207373850700748, 5.000000000000000000 ) ) ;
#5603=DIRECTION ( 'NONE',  ( -0.000000000000000000, -0.000000000000000000, 1.000000000000000000 ) ) ;
#5604=VERTEX_POINT ( 'NONE', #10274 ) ;
#5605=CARTESIAN_POINT ( 'NONE',  ( 3.328169399223510627, 5.259292476615662792, 4.000000000000000000 ) ) ;
#5606=ORIENTED_EDGE ( 'NONE', *, *, #16978, .T. ) ;
#5607=EDGE_CURVE ( 'NONE', #14862, #70976, #98023, .T. ) ;
#5608=ORIENTED_EDGE ( 'NONE', *, *, #50535, .T. ) ;
#5610=ORIENTED_EDGE ( 'NONE', *, *, #167, .T. ) ;
#5611=VERTEX_POINT ( 'NONE', #31342 ) ;
#5613=VECTOR ( 'NONE', #126350, 1000.000000000000000 ) ;
#5614=ORIENTED_EDGE ( 'NONE', *, *, #100147, .T. ) ;
#5615=FACE_OUTER_BOUND ( 'NONE', #115634, .T. ) ;
#5616=VECTOR ( 'NONE', #21789, 999.9999999999998863 ) ;
#5617=DIRECTION ( 'NONE',  ( -0.7071067811865486830, 0.7071067811865464625, 0.000000000000000000 ) ) ;
#5619=LINE ( 'NONE', #28118, #100422 ) ;
#5622=CARTESIAN_POINT ( 'NONE',  ( 0.000000000000000000, 0.000000000000000000, 5.000000000000000000 ) ) ;
#5623=DIRECTION ( 'NONE',  ( -0.7071067811865487940, 0.7071067811865463515, 0.000000000000000000 ) ) ;
#5624=PLANE ( 'NONE',  #106928 ) ;
#5626=ORIENTED_EDGE ( 'NONE', *, *, #34573, .F. ) ;
#5629=CARTESIAN_POINT ( 'NONE',  ( -24.29974487139158867, -27.71228299555223273, 4.000000000000000000 ) ) ;
#5630=ORIENTED_EDGE ( 'NONE', *, *, #116140, .F. ) ;
#5631=ORIENTED_EDGE ( 'NONE', *, *, #80022, .F. ) ;
#5632=DIRECTION ( 'NONE',  ( 0.7071067811865487940, 0.7071067811865463515, -0.000000000000000000 ) ) ;
#5633=ORIENTED_EDGE ( 'NONE', *, *, #127103, .F. ) ;
#5634=CARTESIAN_POINT ( 'NONE',  ( 3.489213562373097322, -27.52281430457057709, 5.000000000000000000 ) ) ;
#5636=CARTESIAN_POINT ( 'NONE',  ( 17.99999999999987210, -16.06887692260766087, 4.000000000000000000 ) ) ;
#5637=FACE_OUTER_BOUND ( 'NONE', #51398, .T. ) ;
#5638=ADVANCED_FACE ( 'NONE', ( #64681 ), #100171, .F. ) ;
#5639=VERTEX_POINT ( 'NONE', #41482 ) ;
#5641=ORIENTED_EDGE ( 'NONE', *, *, #109282, .T. ) ;
#5642=VECTOR ( 'NONE', #53429, 1000.000000000000000 ) ;
#5643=EDGE_CURVE ( 'NONE', #33187, #11149, #65421, .T. ) ;
#5644=EDGE_CURVE ( 'NONE', #104233, #106314, #142259, .T. ) ;
#5647=VECTOR ( 'NONE', #84174, 1000.000000000000227 ) ;
#5648=EDGE_CURVE ( 'NONE', #135168, #16747, #32046, .T. ) ;
#5649=CARTESIAN_POINT ( 'NONE',  ( -5.510786437626906675, -27.52281430457051314, 5.000000000000000000 ) ) ;
#5650=LINE ( 'NONE', #50614, #2602 ) ;
#5651=EDGE_LOOP ( 'NONE', ( #62856, #691, #22807, #130085 ) ) ;
#5652=ORIENTED_EDGE ( 'NONE', *, *, #99181, .T. ) ;
#5653=ADVANCED_FACE ( 'NONE', ( #132093 ), #98713, .T. ) ;
#5654=VERTEX_POINT ( 'NONE', #88590 ) ;
#5656=CARTESIAN_POINT ( 'NONE',  ( -34.62823445044363524, -8.240707523384193323, 11.38925528200760695 ) ) ;
#5657=CARTESIAN_POINT ( 'NONE',  ( -13.49999999999990408, 18.43112307739199451, 4.000000000000000000 ) ) ;
#5658=ADVANCED_FACE ( 'NONE', ( #33504 ), #121881, .F. ) ;
#5659=CARTESIAN_POINT ( 'NONE',  ( -33.18398860626899705, 28.73617430169810305, 5.000000000000000000 ) ) ;
#5660=CARTESIAN_POINT ( 'NONE',  ( 22.49999999999985434, 13.56627193232217188, -10.57019076586063555 ) ) ;
#5661=CARTESIAN_POINT ( 'NONE',  ( -50.99451991528749062, 28.92564299267973738, 4.000000000000000000 ) ) ;
#5662=EDGE_CURVE ( 'NONE', #28576, #85226, #61817, .T. ) ;
#5664=ADVANCED_FACE ( 'NONE', ( #81282 ), #113152, .F. ) ;
#5665=LINE ( 'NONE', #47121, #111383 ) ;
#5666=CARTESIAN_POINT ( 'NONE',  ( 25.49999999999981881, 8.900465351122173630, -2.516491619111572930 ) ) ;
#5668=DIRECTION ( 'NONE',  ( 0.7071067811865487940, 0.7071067811865463515, 0.000000000000000000 ) ) ;
#5669=DIRECTION ( 'NONE',  ( 0.7071067811865486830, -0.7071067811865464625, -0.000000000000000000 ) ) ;
#5671=ADVANCED_FACE ( 'NONE', ( #26172 ), #35652, .F. ) ;
#5672=CARTESIAN_POINT ( 'NONE',  ( -34.49999999999976552, 8.319652575858347276, -8.582050562765903834 ) ) ;
#5673=CARTESIAN_POINT ( 'NONE',  ( 34.49999999999975842, -1.535744391599495273, 4.994342998332161443 ) ) ;
#5674=VERTEX_POINT ( 'NONE', #122610 ) ;
#5675=ADVANCED_FACE ( 'NONE', ( #13827 ), #5800, .F. ) ;
#5677=PLANE ( 'NONE',  #101587 ) ;
#5678=EDGE_LOOP ( 'NONE', ( #133052, #110609, #1717, #135772 ) ) ;
#5679=DIRECTION ( 'NONE',  ( 0.000000000000000000, -0.3543493200069153248, -0.9351131265310291818 ) ) ;
#5681=VERTEX_POINT ( 'NONE', #94264 ) ;
#5684=DIRECTION ( 'NONE',  ( -0.6830127018922180770, -0.6830127018922204085, -0.2588190451025213501 ) ) ;
#5686=CARTESIAN_POINT ( 'NONE',  ( -4.499999999999966249, 4.087461875839200509, 4.000000000000000000 ) ) ;
#5687=CARTESIAN_POINT ( 'NONE',  ( 4.828169399223495084, -20.24070752338407431, 4.000000000000000000 ) ) ;
#5688=PLANE ( 'NONE',  #95414 ) ;
#5693=CARTESIAN_POINT ( 'NONE',  ( 9.183988606268997046, 28.73617430169793607, 5.000000000000000000 ) ) ;
#5694=DIRECTION ( 'NONE',  ( -0.000000000000000000, 0.000000000000000000, 1.000000000000000000 ) ) ;
#5696=VERTEX_POINT ( 'NONE', #26869 ) ;
#5697=AXIS2_PLACEMENT_3D ( 'NONE', #63789, #9338, #52863 ) ;
#5698=ORIENTED_EDGE ( 'NONE', *, *, #87684, .F. ) ;
#5702=ORIENTED_EDGE ( 'NONE', *, *, #13266, .T. ) ;
#5703=EDGE_CURVE ( 'NONE', #23510, #95696, #6495, .T. ) ;
#5705=LINE ( 'NONE', #81173, #32482 ) ;
#5706=DIRECTION ( 'NONE',  ( 0.7071067811865487940, 0.7071067811865463515, 0.000000000000000000 ) ) ;
#5707=VERTEX_POINT ( 'NONE', #137797 ) ;
#5708=DIRECTION ( 'NONE',  ( -0.7071067811865486830, -0.7071067811865464625, 0.000000000000000000 ) ) ;
#5710=LINE ( 'NONE', #73163, #95050 ) ;
#5712=CARTESIAN_POINT ( 'NONE',  ( 5.241399257802002332, 21.72500000000000853, 5.000000000000000000 ) ) ;
#5713=DIRECTION ( 'NONE',  ( 0.000000000000000000, -0.3543493200069152138, 0.9351131265310292928 ) ) ;
#5714=LINE ( 'NONE', #138404, #26292 ) ;
#5715=DIRECTION ( 'NONE',  ( 0.7071067811865487940, 0.7071067811865463515, 0.000000000000000000 ) ) ;
#5716=CARTESIAN_POINT ( 'NONE',  ( 20.99451991528748707, 28.92564299267952777, 4.000000000000000000 ) ) ;
#5717=CARTESIAN_POINT ( 'NONE',  ( 34.60343192894621467, -14.24070752338413293, 19.24067776001733776 ) ) ;
#5720=VECTOR ( 'NONE', #20883, 999.9999999999998863 ) ;
#5721=ORIENTED_EDGE ( 'NONE', *, *, #12537, .T. ) ;
#5722=EDGE_LOOP ( 'NONE', ( #75783, #5698, #23656, #100113 ) ) ;
#5724=ORIENTED_EDGE ( 'NONE', *, *, #134703, .F. ) ;
#5725=AXIS2_PLACEMENT_3D ( 'NONE', #16429, #117177, #38929 ) ;
#5726=EDGE_CURVE ( 'NONE', #59180, #33017, #139233, .T. ) ;
#5728=ORIENTED_EDGE ( 'NONE', *, *, #120272, .T. ) ;
#5729=DIRECTION ( 'NONE',  ( 1.000000000000000000, 0.000000000000000000, 0.000000000000000000 ) ) ;
#5730=DIRECTION ( 'NONE',  ( 0.7071067811865487940, 0.7071067811865463515, 0.000000000000000000 ) ) ;
#5734=ADVANCED_FACE ( 'NONE', ( #126877 ), #128348, .F. ) ;
#5736=ORIENTED_EDGE ( 'NONE', *, *, #102296, .F. ) ;
#5737=PLANE ( 'NONE',  #121724 ) ;
#5739=LINE ( 'NONE', #16632, #128812 ) ;
#5740=CARTESIAN_POINT ( 'NONE',  ( 13.82816939922343025, -20.24070752338408496, 4.000000000000000000 ) ) ;
#5741=EDGE_LOOP ( 'NONE', ( #6724, #87544, #126370, #29250 ) ) ;
#5743=EDGE_CURVE ( 'NONE', #4252, #123709, #117421, .T. ) ;
#5744=ORIENTED_EDGE ( 'NONE', *, *, #50492, .F. ) ;
#5745=CARTESIAN_POINT ( 'NONE',  ( -14.99999999999989519, 20.70535890316560312, 1.956823837851950909 ) ) ;
#5746=LINE ( 'NONE', #41246, #63919 ) ;
#5748=CARTESIAN_POINT ( 'NONE',  ( 33.18398860626899705, 28.73617430169810305, 5.000000000000000000 ) ) ;
#5750=VECTOR ( 'NONE', #114755, 1000.000000000000000 ) ;
#5752=DIRECTION ( 'NONE',  ( 0.3543493200069163240, -0.000000000000000000, -0.9351131265310288487 ) ) ;
#5753=ORIENTED_EDGE ( 'NONE', *, *, #87193, .F. ) ;
#5754=VECTOR ( 'NONE', #31131, 1000.000000000000000 ) ;
#5756=LINE ( 'NONE', #8584, #64147 ) ;
#5757=ORIENTED_EDGE ( 'NONE', *, *, #139949, .T. ) ;
#5760=FACE_OUTER_BOUND ( 'NONE', #71463, .T. ) ;
#5762=ADVANCED_FACE ( 'NONE', ( #4334 ), #51501, .F. ) ;
#5763=ORIENTED_EDGE ( 'NONE', *, *, #99810, .F. ) ;
#5765=PLANE ( 'NONE',  #52495 ) ;
#5766=DIRECTION ( 'NONE',  ( -0.3543493200069162685, -0.000000000000000000, -0.9351131265310288487 ) ) ;
#5768=ORIENTED_EDGE ( 'NONE', *, *, #45487, .F. ) ;
#5769=LINE ( 'NONE', #50739, #67213 ) ;
#5770=FACE_BOUND ( 'NONE', #110690, .T. ) ;
#5771=EDGE_LOOP ( 'NONE', ( #92201, #131655, #134228, #23621 ) ) ;
#5772=CARTESIAN_POINT ( 'NONE',  ( 15.48921356237309510, -27.52281430457066236, 5.000000000000000000 ) ) ;
#5773=DIRECTION ( 'NONE',  ( -0.000000000000000000, 0.3543493200069153248, 0.9351131265310292928 ) ) ;
#5774=CARTESIAN_POINT ( 'NONE',  ( -18.48921356237309510, -27.52281430457068367, 5.000000000000000000 ) ) ;
#5775=EDGE_CURVE ( 'NONE', #7970, #127842, #95694, .T. ) ;
#5776=ORIENTED_EDGE ( 'NONE', *, *, #142102, .T. ) ;
#5777=CARTESIAN_POINT ( 'NONE',  ( 38.99451991528749062, 28.92564299267965211, 4.000000000000000000 ) ) ;
#5778=ORIENTED_EDGE ( 'NONE', *, *, #57619, .T. ) ;
#5779=ORIENTED_EDGE ( 'NONE', *, *, #36107, .F. ) ;
#5780=VERTEX_POINT ( 'NONE', #40623 ) ;
#5782=VERTEX_POINT ( 'NONE', #16709 ) ;
#5783=CARTESIAN_POINT ( 'NONE',  ( 0.000000000000000000, 21.72500000000000142, 4.500000000000000888 ) ) ;
#5784=CARTESIAN_POINT ( 'NONE',  ( 23.99451991528749062, 28.92564299267954908, 4.000000000000000000 ) ) ;
#5785=FACE_OUTER_BOUND ( 'NONE', #135149, .T. ) ;
#5786=CARTESIAN_POINT ( 'NONE',  ( 19.49999999999986144, -16.91253812416058366, 4.000000000000000000 ) ) ;
#5787=FACE_OUTER_BOUND ( 'NONE', #91778, .T. ) ;
#5788=FACE_OUTER_BOUND ( 'NONE', #77311, .T. ) ;
#5789=CARTESIAN_POINT ( 'NONE',  ( 9.183988606268997046, 28.73617430169793607, 5.000000000000000000 ) ) ;
#5790=DIRECTION ( 'NONE',  ( 0.6830127018922181881, 0.6830127018922202975, -0.2588190451025214056 ) ) ;
#5791=CARTESIAN_POINT ( 'NONE',  ( 22.49999999999983658, -14.56887692260766620, 4.000000000000000000 ) ) ;
#5792=ORIENTED_EDGE ( 'NONE', *, *, #7677, .T. ) ;
#5793=VERTEX_POINT ( 'NONE', #129033 ) ;
#5794=VERTEX_POINT ( 'NONE', #142089 ) ;
#5795=EDGE_LOOP ( 'NONE', ( #100958, #36759, #91151, #34117 ) ) ;
#5797=EDGE_LOOP ( 'NONE', ( #31914, #143302, #75467, #27848 ) ) ;
#5798=ORIENTED_EDGE ( 'NONE', *, *, #51055, .T. ) ;
#5799=DIRECTION ( 'NONE',  ( -1.000000000000000000, 0.000000000000000000, 0.000000000000000000 ) ) ;
#5800=PLANE ( 'NONE',  #140525 ) ;
#5801=LINE ( 'NONE', #84151, #34735 ) ;
#5802=VERTEX_POINT ( 'NONE', #20258 ) ;
#5803=CARTESIAN_POINT ( 'NONE',  ( -45.18398860626900415, 28.73617430169818832, 5.000000000000000000 ) ) ;
#5804=ORIENTED_EDGE ( 'NONE', *, *, #970, .T. ) ;
#5805=CARTESIAN_POINT ( 'NONE',  ( 2.207106781186521260, -17.24070752338411339, 5.000000000000000000 ) ) ;
#5806=AXIS2_PLACEMENT_3D ( 'NONE', #42515, #65715, #109878 ) ;
#5807=DIRECTION ( 'NONE',  ( -0.7071067811865486830, -0.7071067811865464625, 0.000000000000000000 ) ) ;
#5808=EDGE_CURVE ( 'NONE', #44292, #65489, #142774, .T. ) ;
#5809=ORIENTED_EDGE ( 'NONE', *, *, #100029, .T. ) ;
#5812=EDGE_CURVE ( 'NONE', #82267, #34219, #121713, .T. ) ;
#5813=AXIS2_PLACEMENT_3D ( 'NONE', #73026, #72321, #17856 ) ;
#5816=EDGE_LOOP ( 'NONE', ( #12831, #126658, #73613, #89706 ) ) ;
#5817=ORIENTED_EDGE ( 'NONE', *, *, #12976, .F. ) ;
#5818=EDGE_CURVE ( 'NONE', #69618, #2772, #136177, .T. ) ;
#5819=CARTESIAN_POINT ( 'NONE',  ( -66.48921356237309510, -27.52281430457101763, 5.000000000000000000 ) ) ;
#5821=DIRECTION ( 'NONE',  ( 0.6830127018922181881, 0.6830127018922202975, -0.2588190451025214056 ) ) ;
#5822=DIRECTION ( 'NONE',  ( 0.7071067811865487940, 0.7071067811865463515, 0.000000000000000000 ) ) ;
#5824=EDGE_CURVE ( 'NONE', #4199, #11154, #123900, .T. ) ;
#5825=CARTESIAN_POINT ( 'NONE',  ( -36.29974487139159578, -27.71228299555231445, 4.000000000000000000 ) ) ;
#5826=VERTEX_POINT ( 'NONE', #112303 ) ;
#5827=CARTESIAN_POINT ( 'NONE',  ( 15.70710678118643422, -15.74070752338412760, 5.000000000000000000 ) ) ;
#5828=LINE ( 'NONE', #103552, #119294 ) ;
#5829=VECTOR ( 'NONE', #113026, 1000.000000000000000 ) ;
#5830=CARTESIAN_POINT ( 'NONE',  ( -24.29974487139158867, -27.71228299555223273, 4.000000000000000000 ) ) ;
#5831=DIRECTION ( 'NONE',  ( -0.7071067811865486830, -0.7071067811865464625, 0.000000000000000000 ) ) ;
#5832=EDGE_LOOP ( 'NONE', ( #100433, #111507, #56268, #60240 ) ) ;
#5833=CARTESIAN_POINT ( 'NONE',  ( -14.99999999999989875, -1.209798855135683748, 4.371887122346860721 ) ) ;
#5834=CARTESIAN_POINT ( 'NONE',  ( 2.816011393730999401, 28.73617430169785436, 5.000000000000000000 ) ) ;
#5835=ORIENTED_EDGE ( 'NONE', *, *, #25142, .T. ) ;
#5837=CARTESIAN_POINT ( 'NONE',  ( -5.903329358125916748, -2.240707523384260824, 15.26439735382751195 ) ) ;
#5838=ORIENTED_EDGE ( 'NONE', *, *, #126830, .T. ) ;
#5839=EDGE_CURVE ( 'NONE', #21613, #21499, #81109, .T. ) ;
#5843=ORIENTED_EDGE ( 'NONE', *, *, #121000, .T. ) ;
#5844=LINE ( 'NONE', #61715, #30373 ) ;
#5846=ADVANCED_FACE ( 'NONE', ( #11508 ), #55790, .F. ) ;
#5847=VECTOR ( 'NONE', #121093, 1000.000000000000227 ) ;
#5848=DIRECTION ( 'NONE',  ( -0.7071067811865486830, -0.7071067811865464625, 0.000000000000000000 ) ) ;
#5850=CARTESIAN_POINT ( 'NONE',  ( -28.43312800248725125, -21.74070752338406365, 6.915939825044140399 ) ) ;
#5851=VERTEX_POINT ( 'NONE', #6323 ) ;
#5852=FACE_OUTER_BOUND ( 'NONE', #69100, .T. ) ;
#5853=CARTESIAN_POINT ( 'NONE',  ( -33.72281430457037743, -21.72499999999999432, 5.000000000000000000 ) ) ;
#5854=FACE_OUTER_BOUND ( 'NONE', #83506, .T. ) ;
#5855=CARTESIAN_POINT ( 'NONE',  ( -2.816011393730999401, 28.73617430169785436, 5.000000000000000000 ) ) ;
#5856=CARTESIAN_POINT ( 'NONE',  ( 72.18398860626899705, 28.73617430169837661, 5.000000000000000000 ) ) ;
#5857=EDGE_CURVE ( 'NONE', #104032, #131707, #137625, .T. ) ;
#5859=DIRECTION ( 'NONE',  ( -0.000000000000000000, 0.000000000000000000, 1.000000000000000000 ) ) ;
#5861=CARTESIAN_POINT ( 'NONE',  ( -60.48921356237309510, -27.52281430457097500, 5.000000000000000000 ) ) ;
#5862=ORIENTED_EDGE ( 'NONE', *, *, #137011, .F. ) ;
#5863=ORIENTED_EDGE ( 'NONE', *, *, #117573, .T. ) ;
#5864=ORIENTED_EDGE ( 'NONE', *, *, #31052, .F. ) ;
#5866=ORIENTED_EDGE ( 'NONE', *, *, #57115, .F. ) ;
#5867=ORIENTED_EDGE ( 'NONE', *, *, #121527, .T. ) ;
#5868=ORIENTED_EDGE ( 'NONE', *, *, #126098, .F. ) ;
#5869=EDGE_CURVE ( 'NONE', #118949, #14811, #5828, .T. ) ;
#5872=DIRECTION ( 'NONE',  ( 0.000000000000000000, 0.000000000000000000, 1.000000000000000000 ) ) ;
#5873=PLANE ( 'NONE',  #21001 ) ;
#5874=PLANE ( 'NONE',  #51098 ) ;
#5875=PLANE ( 'NONE',  #37181 ) ;
#5877=ORIENTED_EDGE ( 'NONE', *, *, #39549, .F. ) ;
#5879=DIRECTION ( 'NONE',  ( 0.7071067811865487940, -0.7071067811865463515, 0.000000000000000000 ) ) ;
#5880=PLANE ( 'NONE',  #68208 ) ;
#5881=CARTESIAN_POINT ( 'NONE',  ( -29.99451991528749417, 28.92564299267958816, 4.000000000000000000 ) ) ;
#5882=DIRECTION ( 'NONE',  ( -0.7071067811865486830, -0.7071067811865464625, -0.000000000000000000 ) ) ;
#5883=PLANE ( 'NONE',  #138044 ) ;
#5885=ADVANCED_FACE ( 'NONE', ( #58535 ), #93952, .F. ) ;
#5886=CARTESIAN_POINT ( 'NONE',  ( -14.91685193227060324, 21.75929247661549937, 7.311836541448015758 ) ) ;
#5888=ORIENTED_EDGE ( 'NONE', *, *, #21651, .F. ) ;
#5889=ORIENTED_EDGE ( 'NONE', *, *, #92510, .F. ) ;
#5891=ORIENTED_EDGE ( 'NONE', *, *, #50407, .F. ) ;
#5893=DIRECTION ( 'NONE',  ( -0.7071067811865486830, -0.7071067811865464625, 0.000000000000000000 ) ) ;
#5894=PLANE ( 'NONE',  #45753 ) ;
#5895=CARTESIAN_POINT ( 'NONE',  ( 32.20710678118632586, -11.24070752338416845, 5.000000000000000000 ) ) ;
#5896=DIRECTION ( 'NONE',  ( -0.6830127018922180770, -0.6830127018922204085, -0.2588190451025213501 ) ) ;
#5897=DIRECTION ( 'NONE',  ( 0.6830127018922181881, 0.6830127018922202975, -0.2588190451025214056 ) ) ;
#5899=VERTEX_POINT ( 'NONE', #30428 ) ;
#5900=EDGE_CURVE ( 'NONE', #108030, #94785, #76072, .T. ) ;
#5902=EDGE_LOOP ( 'NONE', ( #46119, #25945, #122339, #12117 ) ) ;
#5903=CARTESIAN_POINT ( 'NONE',  ( -15.48921356237309510, -27.52281430457066236, 5.000000000000000000 ) ) ;
#5904=LINE ( 'NONE', #138613, #112472 ) ;
#5905=CARTESIAN_POINT ( 'NONE',  ( -2.999999999999976463, 4.552185695429124657, 5.000000000000000000 ) ) ;
#5906=DIRECTION ( 'NONE',  ( 0.6830127018922181881, 0.6830127018922202975, -0.2588190451025214056 ) ) ;
#5909=ADVANCED_FACE ( 'NONE', ( #65942 ), #10085, .F. ) ;
#5910=ORIENTED_EDGE ( 'NONE', *, *, #132851, .F. ) ;
#5911=DIRECTION ( 'NONE',  ( 0.6830127018922180770, -0.6830127018922204085, -0.2588190451025213501 ) ) ;
#5912=CARTESIAN_POINT ( 'NONE',  ( 75.48921356237309510, -27.52281430457107803, 5.000000000000000000 ) ) ;
#5913=CARTESIAN_POINT ( 'NONE',  ( 31.49999999999977973, -17.91344420646039737, 1.358650452708537681 ) ) ;
#5914=LINE ( 'NONE', #5212, #141294 ) ;
#5915=VECTOR ( 'NONE', #91011, 999.9999999999998863 ) ;
#5917=ORIENTED_EDGE ( 'NONE', *, *, #56181, .T. ) ;
#5918=AXIS2_PLACEMENT_3D ( 'NONE', #41789, #131659, #107027 ) ;
#5919=DIRECTION ( 'NONE',  ( -0.000000000000000000, -0.3543493200069152693, 0.9351131265310292928 ) ) ;
#5920=ADVANCED_FACE ( 'NONE', ( #31156 ), #142753, .T. ) ;
#5921=PLANE ( 'NONE',  #124260 ) ;
#5922=ORIENTED_EDGE ( 'NONE', *, *, #40593, .T. ) ;
#5923=ORIENTED_EDGE ( 'NONE', *, *, #16193, .T. ) ;
#5924=LINE ( 'NONE', #6621, #28476 ) ;
#5925=VERTEX_POINT ( 'NONE', #55048 ) ;
#5926=( BOUNDED_CURVE ( )  B_SPLINE_CURVE ( 3, ( #20520, #12519, #44480, #100959 ),
 .UNSPECIFIED., .F., .F. ) 
 B_SPLINE_CURVE_WITH_KNOTS ( ( 4, 4 ),
 ( 6.095931195673056635, 6.243513561394028244 ),
 .UNSPECIFIED. ) 
 CURVE ( )  GEOMETRIC_REPRESENTATION_ITEM ( )  RATIONAL_B_SPLINE_CURVE ( ( 1.000000000000000000, 0.9981857772260753769, 0.9981857772260753769, 1.000000000000000000 ) ) 
 REPRESENTATION_ITEM ( '' )  );
#5928=EDGE_CURVE ( 'NONE', #35299, #133165, #139923, .T. ) ;
#5929=ORIENTED_EDGE ( 'NONE', *, *, #63416, .F. ) ;
#5930=CARTESIAN_POINT ( 'NONE',  ( 22.49999999999984723, -4.533600742197692490, 5.000000000000000000 ) ) ;
#5932=EDGE_CURVE ( 'NONE', #77443, #96830, #77525, .T. ) ;
#5933=FACE_BOUND ( 'NONE', #118698, .T. ) ;
#5934=CARTESIAN_POINT ( 'NONE',  ( -27.29974487139158512, -27.71228299555225405, 4.000000000000000000 ) ) ;
#5936=CARTESIAN_POINT ( 'NONE',  ( 21.48921356237309155, -27.52281430457070499, 5.000000000000000000 ) ) ;
#5937=EDGE_CURVE ( 'NONE', #140592, #131858, #101384, .T. ) ;
#5938=ORIENTED_EDGE ( 'NONE', *, *, #40608, .T. ) ;
#5939=CARTESIAN_POINT ( 'NONE',  ( -2.999999999999978240, -3.485240976185081330, -4.108735105802402643 ) ) ;
#5940=DIRECTION ( 'NONE',  ( 0.000000000000000000, 0.000000000000000000, 1.000000000000000000 ) ) ;
#5941=VERTEX_POINT ( 'NONE', #2029 ) ;
#5942=ORIENTED_EDGE ( 'NONE', *, *, #80045, .T. ) ;
#5943=DIRECTION ( 'NONE',  ( -0.6830127018922181881, 0.6830127018922202975, -0.2588190451025214056 ) ) ;
#5946=VECTOR ( 'NONE', #140047, 1000.000000000000000 ) ;
#5947=ORIENTED_EDGE ( 'NONE', *, *, #92590, .T. ) ;
#5949=VERTEX_POINT ( 'NONE', #68790 ) ;
#5951=PLANE ( 'NONE',  #88052 ) ;
#5953=CARTESIAN_POINT ( 'NONE',  ( 21.18398860626899349, 28.73617430169802134, 5.000000000000000000 ) ) ;
#5954=ORIENTED_EDGE ( 'NONE', *, *, #68503, .F. ) ;
#5956=EDGE_CURVE ( 'NONE', #39954, #101036, #102117, .T. ) ;
#5957=CARTESIAN_POINT ( 'NONE',  ( -15.48921356237309510, -27.52281430457066236, 5.000000000000000000 ) ) ;
#5958=CARTESIAN_POINT ( 'NONE',  ( -19.49999999999986855, -11.56887692260769640, 4.000000000000000000 ) ) ;
#5959=DIRECTION ( 'NONE',  ( 0.7071067811865487940, 0.7071067811865463515, -0.000000000000000000 ) ) ;
#5960=DIRECTION ( 'NONE',  ( -0.7071067811865486830, -0.7071067811865464625, 0.000000000000000000 ) ) ;
#5961=LINE ( 'NONE', #18264, #74063 ) ;
#5962=EDGE_LOOP ( 'NONE', ( #71684, #83183, #137721, #5744 ) ) ;
#5963=ORIENTED_EDGE ( 'NONE', *, *, #120606, .F. ) ;
#5964=DIRECTION ( 'NONE',  ( 0.7071067811865487940, 0.7071067811865463515, 0.000000000000000000 ) ) ;
#5965=CARTESIAN_POINT ( 'NONE',  ( -5.700255128608413102, -27.71228299555201957, 4.000000000000000000 ) ) ;
#5966=VERTEX_POINT ( 'NONE', #16495 ) ;
#5967=ORIENTED_EDGE ( 'NONE', *, *, #74661, .T. ) ;
#5968=VERTEX_POINT ( 'NONE', #104210 ) ;
#5970=LINE ( 'NONE', #138687, #77635 ) ;
#5971=CARTESIAN_POINT ( 'NONE',  ( -22.25154412867562215, -11.24070752338416845, 10.39518518046014428 ) ) ;
#5973=DIRECTION ( 'NONE',  ( -0.7071067811865487940, 0.7071067811865463515, -0.000000000000000000 ) ) ;
#5976=EDGE_CURVE ( 'NONE', #49913, #55910, #118498, .T. ) ;
#5977=DIRECTION ( 'NONE',  ( -0.000000000000000000, 0.000000000000000000, 1.000000000000000000 ) ) ;
#5978=ORIENTED_EDGE ( 'NONE', *, *, #78620, .F. ) ;
#5979=EDGE_CURVE ( 'NONE', #119189, #126916, #98194, .T. ) ;
#5980=CARTESIAN_POINT ( 'NONE',  ( -15.70710678118642711, -9.740707523384180888, 5.000000000000000000 ) ) ;
#5982=CARTESIAN_POINT ( 'NONE',  ( -51.29974487139158867, -27.71228299555242103, 4.000000000000000000 ) ) ;
#5984=LINE ( 'NONE', #93755, #114184 ) ;
#5985=ORIENTED_EDGE ( 'NONE', *, *, #11317, .F. ) ;
#5986=DIRECTION ( 'NONE',  ( 0.3543493200069162685, -0.000000000000000000, -0.9351131265310288487 ) ) ;
#5987=LINE ( 'NONE', #124946, #104760 ) ;
#5988=ADVANCED_FACE ( 'NONE', ( #88763 ), #64140, .F. ) ;
#5989=EDGE_CURVE ( 'NONE', #13100, #65062, #2409, .T. ) ;
#5991=VERTEX_POINT ( 'NONE', #113325 ) ;
#5992=FACE_OUTER_BOUND ( 'NONE', #113046, .T. ) ;
#5993=DIRECTION ( 'NONE',  ( -0.7071067811865486830, -0.7071067811865464625, -0.000000000000000000 ) ) ;
#5995=DIRECTION ( 'NONE',  ( 0.6830127018922181881, 0.6830127018922202975, -0.2588190451025214056 ) ) ;
#5996=ORIENTED_EDGE ( 'NONE', *, *, #102459, .T. ) ;
#5997=CARTESIAN_POINT ( 'NONE',  ( -2.999999999999988898, 20.58746187583904330, 4.000000000000000000 ) ) ;
#5999=LINE ( 'NONE', #50275, #16807 ) ;
#6000=CARTESIAN_POINT ( 'NONE',  ( 15.29974487139158867, -27.71228299555216879, 4.000000000000000000 ) ) ;
#6003=EDGE_LOOP ( 'NONE', ( #90568, #40275, #8693, #76532 ) ) ;
#6004=EDGE_CURVE ( 'NONE', #13171, #10686, #5970, .T. ) ;
#6005=ORIENTED_EDGE ( 'NONE', *, *, #33335, .F. ) ;
#6006=CARTESIAN_POINT ( 'NONE',  ( -28.49999999999980105, -7.912538124160673370, 4.000000000000000000 ) ) ;
#6009=AXIS2_PLACEMENT_3D ( 'NONE', #102249, #137001, #104341 ) ;
#6011=PLANE ( 'NONE',  #87804 ) ;
#6012=CARTESIAN_POINT ( 'NONE',  ( 17.99451991528748351, 28.92564299267950645, 4.000000000000000000 ) ) ;
#6014=CARTESIAN_POINT ( 'NONE',  ( -20.99451991528748707, 28.92564299267952777, 4.000000000000000000 ) ) ;
#6015=ORIENTED_EDGE ( 'NONE', *, *, #40694, .F. ) ;
#6016=CARTESIAN_POINT ( 'NONE',  ( -34.42500000000001137, -15.02281430457042077, 5.000000000000000000 ) ) ;
#6017=DIRECTION ( 'NONE',  ( 0.7071067811865486830, -0.7071067811865464625, -0.000000000000000000 ) ) ;
#6018=DIRECTION ( 'NONE',  ( 0.7071067811865486830, -0.7071067811865464625, -0.000000000000000000 ) ) ;
#6019=ADVANCED_FACE ( 'NONE', ( #51671 ), #49552, .F. ) ;
#6020=DIRECTION ( 'NONE',  ( -0.000000000000000000, 0.000000000000000000, 1.000000000000000000 ) ) ;
#6023=VERTEX_POINT ( 'NONE', #39375 ) ;
#6025=VERTEX_POINT ( 'NONE', #52363 ) ;
#6026=AXIS2_PLACEMENT_3D ( 'NONE', #130914, #131611, #73658 ) ;
#6027=ORIENTED_EDGE ( 'NONE', *, *, #62008, .F. ) ;
#6028=EDGE_CURVE ( 'NONE', #107292, #25402, #140785, .T. ) ;
#6029=DIRECTION ( 'NONE',  ( 0.7071067811865487940, -0.7071067811865463515, 0.000000000000000000 ) ) ;
#6030=LINE ( 'NONE', #83671, #34674 ) ;
#6031=LINE ( 'NONE', #37285, #125268 ) ;
#6032=CARTESIAN_POINT ( 'NONE',  ( 34.92499999999998295, -5.240707523384228850, 4.255531930566196941 ) ) ;
#6033=CARTESIAN_POINT ( 'NONE',  ( -24.91272823266826109, 2.053671025133813277, 5.000000000000000000 ) ) ;
#6034=LINE ( 'NONE', #93094, #82455 ) ;
#6035=VERTEX_POINT ( 'NONE', #140071 ) ;
#6036=EDGE_CURVE ( 'NONE', #39260, #64733, #97975, .T. ) ;
#6037=DIRECTION ( 'NONE',  ( 0.6830127018922181881, 0.6830127018922202975, -0.2588190451025214056 ) ) ;
#6038=LINE ( 'NONE', #47502, #39923 ) ;
#6040=LINE ( 'NONE', #40860, #140466 ) ;
#6041=DIRECTION ( 'NONE',  ( -0.6830127018922181881, 0.6830127018922202975, -0.2588190451025214056 ) ) ;
#6043=DIRECTION ( 'NONE',  ( -0.7071067811865486830, -0.7071067811865464625, 0.000000000000000000 ) ) ;
#6044=VECTOR ( 'NONE', #132218, 1000.000000000000227 ) ;
#6045=VECTOR ( 'NONE', #116093, 1000.000000000000000 ) ;
#6047=EDGE_CURVE ( 'NONE', #120101, #135455, #129060, .T. ) ;
#6048=VECTOR ( 'NONE', #117323, 1000.000000000000000 ) ;
#6050=ORIENTED_EDGE ( 'NONE', *, *, #122077, .T. ) ;
#6051=ORIENTED_EDGE ( 'NONE', *, *, #2027, .T. ) ;
#6053=CARTESIAN_POINT ( 'NONE',  ( -26.67183060077628554, 8.259292476615630818, 4.000000000000000000 ) ) ;
#6054=CARTESIAN_POINT ( 'NONE',  ( -60.29974487139158867, -27.71228299555248142, 4.000000000000000000 ) ) ;
#6055=VECTOR ( 'NONE', #21036, 1000.000000000000227 ) ;
#6056=ORIENTED_EDGE ( 'NONE', *, *, #140735, .T. ) ;
#6057=ADVANCED_FACE ( 'NONE', ( #130627 ), #97215, .T. ) ;
#6058=CARTESIAN_POINT ( 'NONE',  ( -30.90450307870169766, 22.22500000000000142, 3.476483422452860239 ) ) ;
#6063=ORIENTED_EDGE ( 'NONE', *, *, #71013, .T. ) ;
#6064=DIRECTION ( 'NONE',  ( -0.000000000000000000, -0.3543493200069152693, 0.9351131265310292928 ) ) ;
#6065=CARTESIAN_POINT ( 'NONE',  ( 15.18398860626900237, 28.73617430169797871, 5.000000000000000000 ) ) ;
#6066=FACE_OUTER_BOUND ( 'NONE', #64628, .T. ) ;
#6067=DIRECTION ( 'NONE',  ( -0.7071067811865486830, -0.7071067811865464625, 0.000000000000000000 ) ) ;
#6068=CARTESIAN_POINT ( 'NONE',  ( -24.18398860626899705, 28.73617430169804265, 5.000000000000000000 ) ) ;
#6070=EDGE_LOOP ( 'NONE', ( #28776, #43217, #123868, #124565 ) ) ;
#6071=DIRECTION ( 'NONE',  ( 0.6830127018922181881, 0.6830127018922202975, -0.2588190451025214056 ) ) ;
#6072=CARTESIAN_POINT ( 'NONE',  ( 32.99451991528749062, 28.92564299267960948, 4.000000000000000000 ) ) ;
#6075=CARTESIAN_POINT ( 'NONE',  ( 77.99451991528749772, 28.92564299267992567, 4.000000000000000000 ) ) ;
#6076=EDGE_LOOP ( 'NONE', ( #4019, #108807, #56374, #62669 ) ) ;
#6079=( BOUNDED_CURVE ( )  B_SPLINE_CURVE ( 3, ( #113315, #130476, #114044, #40607 ),
 .UNSPECIFIED., .F., .T. ) 
 B_SPLINE_CURVE_WITH_KNOTS ( ( 4, 4 ),
 ( 1.864375635226932282, 1.933014472006554740 ),
 .UNSPECIFIED. ) 
 CURVE ( )  GEOMETRIC_REPRESENTATION_ITEM ( )  RATIONAL_B_SPLINE_CURVE ( ( 1.000000000000000000, 0.9996074310407762065, 0.9996074310407762065, 1.000000000000000000 ) ) 
 REPRESENTATION_ITEM ( '' )  );
#6080=CARTESIAN_POINT ( 'NONE',  ( -20.99999999999985079, 16.93112307739201583, 4.000000000000000000 ) ) ;
#6081=LINE ( 'NONE', #140907, #51084 ) ;
#6082=LINE ( 'NONE', #50357, #24737 ) ;
#6083=EDGE_CURVE ( 'NONE', #106022, #65082, #76223, .T. ) ;
#6086=ORIENTED_EDGE ( 'NONE', *, *, #57634, .T. ) ;
#6087=VECTOR ( 'NONE', #58225, 1000.000000000000000 ) ;
#6089=ORIENTED_EDGE ( 'NONE', *, *, #35438, .F. ) ;
#6090=VERTEX_POINT ( 'NONE', #52316 ) ;
#6091=PLANE ( 'NONE',  #88476 ) ;
#6092=ORIENTED_EDGE ( 'NONE', *, *, #14896, .T. ) ;
#6093=DIRECTION ( 'NONE',  ( -0.000000000000000000, 0.000000000000000000, 1.000000000000000000 ) ) ;
#6094=DIRECTION ( 'NONE',  ( -0.6830127018922181881, 0.6830127018922202975, -0.2588190451025214056 ) ) ;
#6095=VECTOR ( 'NONE', #88825, 1000.000000000000000 ) ;
#6096=ADVANCED_FACE ( 'NONE', ( #31996 ), #120389, .F. ) ;
#6097=FACE_BOUND ( 'NONE', #23335, .T. ) ;
#6098=CARTESIAN_POINT ( 'NONE',  ( 21.18398860626899349, 28.73617430169802134, 5.000000000000000000 ) ) ;
#6101=ORIENTED_EDGE ( 'NONE', *, *, #65636, .T. ) ;
#6102=( BOUNDED_CURVE ( )  B_SPLINE_CURVE ( 3, ( #120506, #140851, #85769, #87212 ),
 .UNSPECIFIED., .F., .F. ) 
 B_SPLINE_CURVE_WITH_KNOTS ( ( 4, 4 ),
 ( 3.794322559382540927, 3.828945978481788526 ),
 .UNSPECIFIED. ) 
 CURVE ( )  GEOMETRIC_REPRESENTATION_ITEM ( )  RATIONAL_B_SPLINE_CURVE ( ( 1.000000000000000000, 0.9999001040657221617, 0.9999001040657221617, 1.000000000000000000 ) ) 
 REPRESENTATION_ITEM ( '' )  );
#6103=EDGE_CURVE ( 'NONE', #72705, #8853, #13776, .T. ) ;
#6107=VERTEX_POINT ( 'NONE', #769 ) ;
#6109=ORIENTED_EDGE ( 'NONE', *, *, #28072, .F. ) ;
#6111=ADVANCED_FACE ( 'NONE', ( #56658 ), #32, .F. ) ;
#6112=FACE_OUTER_BOUND ( 'NONE', #73549, .T. ) ;
#6114=FACE_OUTER_BOUND ( 'NONE', #5816, .T. ) ;
#6115=LINE ( 'NONE', #27188, #121942 ) ;
#6116=EDGE_CURVE ( 'NONE', #76142, #127787, #47218, .T. ) ;
#6117=CARTESIAN_POINT ( 'NONE',  ( 2.999999999999983569, 20.70535890316561733, 1.956823837851910053 ) ) ;
#6118=ORIENTED_EDGE ( 'NONE', *, *, #114527, .T. ) ;
#6119=CARTESIAN_POINT ( 'NONE',  ( 4.499999999999977796, 3.052185695429134871, 5.000000000000000000 ) ) ;
#6120=CARTESIAN_POINT ( 'NONE',  ( 9.299744871391588674, -27.71228299555212971, 4.000000000000000000 ) ) ;
#6121=VECTOR ( 'NONE', #80189, 1000.000000000000000 ) ;
#6122=FACE_OUTER_BOUND ( 'NONE', #135234, .T. ) ;
#6123=DIRECTION ( 'NONE',  ( -1.000000000000000000, -1.743732761913359971E-15, 0.000000000000000000 ) ) ;
#6124=DIRECTION ( 'NONE',  ( 1.000000000000000000, 0.000000000000000000, 0.000000000000000000 ) ) ;
#6125=DIRECTION ( 'NONE',  ( 0.000000000000000000, 1.000000000000000000, -0.000000000000000000 ) ) ;
#6128=CARTESIAN_POINT ( 'NONE',  ( 9.183988606268997046, 28.73617430169793607, 5.000000000000000000 ) ) ;
#6129=ORIENTED_EDGE ( 'NONE', *, *, #106107, .T. ) ;
#6130=DIRECTION ( 'NONE',  ( 0.7071067811865487940, 0.7071067811865463515, 0.000000000000000000 ) ) ;
#6131=CARTESIAN_POINT ( 'NONE',  ( 4.499999999999972466, 16.08746187583908238, 4.000000000000000000 ) ) ;
#6132=ORIENTED_EDGE ( 'NONE', *, *, #33506, .T. ) ;
#6133=VECTOR ( 'NONE', #96664, 1000.000000000000000 ) ;
#6134=ORIENTED_EDGE ( 'NONE', *, *, #94707, .F. ) ;
#6135=ORIENTED_EDGE ( 'NONE', *, *, #123913, .T. ) ;
#6138=VERTEX_POINT ( 'NONE', #11635 ) ;
#6140=VECTOR ( 'NONE', #38596, 1000.000000000000227 ) ;
#6145=LINE ( 'NONE', #93904, #10938 ) ;
#6146=EDGE_CURVE ( 'NONE', #86443, #122293, #88543, .T. ) ;
#6147=ORIENTED_EDGE ( 'NONE', *, *, #11903, .T. ) ;
#6148=CARTESIAN_POINT ( 'NONE',  ( 63.18398860626900415, 28.73617430169831621, 5.000000000000000000 ) ) ;
#6149=AXIS2_PLACEMENT_3D ( 'NONE', #78136, #108558, #120151 ) ;
#6150=DIRECTION ( 'NONE',  ( 0.7071067811865486830, -0.7071067811865464625, -0.000000000000000000 ) ) ;
#6151=LINE ( 'NONE', #49733, #139709 ) ;
#6152=ORIENTED_EDGE ( 'NONE', *, *, #93674, .F. ) ;
#6153=ORIENTED_EDGE ( 'NONE', *, *, #83552, .T. ) ;
#6154=DIRECTION ( 'NONE',  ( -0.000000000000000000, -0.3543493200069152693, 0.9351131265310292928 ) ) ;
#6155=LINE ( 'NONE', #86453, #57459 ) ;
#6156=ADVANCED_FACE ( 'NONE', ( #21834 ), #91397, .F. ) ;
#6158=ORIENTED_EDGE ( 'NONE', *, *, #12075, .F. ) ;
#6159=PLANE ( 'NONE',  #62078 ) ;
#6161=VERTEX_POINT ( 'NONE', #90684 ) ;
#6162=EDGE_LOOP ( 'NONE', ( #135687, #45480, #50369 ) ) ;
#6163=ORIENTED_EDGE ( 'NONE', *, *, #38798, .T. ) ;
#6164=CARTESIAN_POINT ( 'NONE',  ( -16.49999999999988987, 10.08746187583914633, 4.000000000000000000 ) ) ;
#6165=ADVANCED_FACE ( 'NONE', ( #22514 ), #134917, .F. ) ;
#6166=CARTESIAN_POINT ( 'NONE',  ( 0.000000000000000000, 0.000000000000000000, 5.000000000000000000 ) ) ;
#6167=CARTESIAN_POINT ( 'NONE',  ( 45.29974487139158867, -27.71228299555237840, 4.000000000000000000 ) ) ;
#6168=EDGE_CURVE ( 'NONE', #124077, #55125, #124013, .T. ) ;
#6169=DIRECTION ( 'NONE',  ( -0.7071067811865486830, -0.7071067811865464625, -0.000000000000000000 ) ) ;
#6170=ORIENTED_EDGE ( 'NONE', *, *, #130276, .T. ) ;
#6172=ORIENTED_EDGE ( 'NONE', *, *, #59400, .T. ) ;
#6173=CARTESIAN_POINT ( 'NONE',  ( 48.18398860626899705, 28.73617430169820608, 5.000000000000000000 ) ) ;
#6175=FACE_OUTER_BOUND ( 'NONE', #10922, .T. ) ;
#6176=AXIS2_PLACEMENT_3D ( 'NONE', #9184, #290, #88785 ) ;
#6178=ADVANCED_FACE ( 'NONE', ( #14530 ), #58808, .F. ) ;
#6179=DIRECTION ( 'NONE',  ( -0.6830127018922180770, -0.6830127018922204085, -0.2588190451025213501 ) ) ;
#6180=VERTEX_POINT ( 'NONE', #113833 ) ;
#6181=VERTEX_POINT ( 'NONE', #3610 ) ;
#6182=ORIENTED_EDGE ( 'NONE', *, *, #88186, .F. ) ;
#6183=DIRECTION ( 'NONE',  ( 0.7071067811865486830, -0.7071067811865464625, -0.000000000000000000 ) ) ;
#6184=DIRECTION ( 'NONE',  ( 0.7071067811865486830, -0.7071067811865464625, -0.000000000000000000 ) ) ;
#6185=CARTESIAN_POINT ( 'NONE',  ( 0.7070132642930391231, -21.74070752338405654, 4.999753212805213565 ) ) ;
#6186=CARTESIAN_POINT ( 'NONE',  ( -2.207106781186525701, -5.240707523384230626, 5.000000000000000000 ) ) ;
#6187=EDGE_CURVE ( 'NONE', #46869, #21681, #47903, .T. ) ;
#6190=FACE_OUTER_BOUND ( 'NONE', #119830, .T. ) ;
#6191=DIRECTION ( 'NONE',  ( -0.000000000000000000, -0.3543493200069152693, 0.9351131265310292928 ) ) ;
#6192=LINE ( 'NONE', #125158, #14783 ) ;
#6193=CARTESIAN_POINT ( 'NONE',  ( 9.183988606268997046, 28.73617430169793607, 5.000000000000000000 ) ) ;
#6194=CARTESIAN_POINT ( 'NONE',  ( -33.18398860626899705, 28.73617430169810305, 5.000000000000000000 ) ) ;
#6195=EDGE_LOOP ( 'NONE', ( #37305, #94825, #34967, #140249 ) ) ;
#6196=LINE ( 'NONE', #104837, #49994 ) ;
#6197=ORIENTED_EDGE ( 'NONE', *, *, #121037, .T. ) ;
#6198=LINE ( 'NONE', #53309, #64677 ) ;
#6199=FACE_OUTER_BOUND ( 'NONE', #116966, .T. ) ;
#6200=ORIENTED_EDGE ( 'NONE', *, *, #115474, .F. ) ;
#6201=VECTOR ( 'NONE', #88374, 1000.000000000000227 ) ;
#6202=CARTESIAN_POINT ( 'NONE',  ( 34.42499999999998295, -21.72500000000000142, 0.5000000000000000000 ) ) ;
#6203=CARTESIAN_POINT ( 'NONE',  ( -6.005480084712508493, 28.92564299267933947, 4.000000000000000000 ) ) ;
#6204=ORIENTED_EDGE ( 'NONE', *, *, #41484, .F. ) ;
#6205=ORIENTED_EDGE ( 'NONE', *, *, #103164, .F. ) ;
#6206=CARTESIAN_POINT ( 'NONE',  ( 27.18398860626900060, 28.73617430169806042, 5.000000000000000000 ) ) ;
#6207=CARTESIAN_POINT ( 'NONE',  ( 27.48921356237309155, -27.52281430457074762, 5.000000000000000000 ) ) ;
#6208=DIRECTION ( 'NONE',  ( 4.681814790819592407E-17, 0.3543493200069153248, 0.9351131265310292928 ) ) ;
#6209=VECTOR ( 'NONE', #133495, 999.9999999999998863 ) ;
#6210=EDGE_CURVE ( 'NONE', #111332, #130548, #89267, .T. ) ;
#6212=LINE ( 'NONE', #94675, #2308 ) ;
#6213=ADVANCED_FACE ( 'NONE', ( #124715 ), #21277, .F. ) ;
#6216=VECTOR ( 'NONE', #35953, 1000.000000000000000 ) ;
#6218=PLANE ( 'NONE',  #87762 ) ;
#6220=DIRECTION ( 'NONE',  ( -0.7071067811865486830, -0.7071067811865464625, 0.000000000000000000 ) ) ;
#6221=LINE ( 'NONE', #38203, #5010 ) ;
#6222=VERTEX_POINT ( 'NONE', #53173 ) ;
#6223=LINE ( 'NONE', #5531, #97737 ) ;
#6224=ORIENTED_EDGE ( 'NONE', *, *, #69725, .F. ) ;
#6226=DIRECTION ( 'NONE',  ( -0.6830127018922180770, -0.6830127018922204085, -0.2588190451025213501 ) ) ;
#6227=CARTESIAN_POINT ( 'NONE',  ( -34.92500000000001137, -22.22500000000000142, 4.000000000000000000 ) ) ;
#6228=LINE ( 'NONE', #115706, #78026 ) ;
#6229=ORIENTED_EDGE ( 'NONE', *, *, #125512, .T. ) ;
#6230=CARTESIAN_POINT ( 'NONE',  ( -60.48921356237309510, -27.52281430457097500, 5.000000000000000000 ) ) ;
#6231=LINE ( 'NONE', #71554, #122907 ) ;
#6233=DIRECTION ( 'NONE',  ( -0.000000000000000000, 0.3543493200069153248, 0.9351131265310291818 ) ) ;
#6234=ORIENTED_EDGE ( 'NONE', *, *, #6647, .T. ) ;
#6235=PLANE ( 'NONE',  #122501 ) ;
#6237=VECTOR ( 'NONE', #76152, 1000.000000000000227 ) ;
#6240=VERTEX_POINT ( 'NONE', #51779 ) ;
#6241=ORIENTED_EDGE ( 'NONE', *, *, #53739, .F. ) ;
#6242=AXIS2_PLACEMENT_3D ( 'NONE', #58229, #46643, #2324 ) ;
#6244=ORIENTED_EDGE ( 'NONE', *, *, #137133, .F. ) ;
#6245=DIRECTION ( 'NONE',  ( 0.000000000000000000, 0.000000000000000000, 1.000000000000000000 ) ) ;
#6247=ADVANCED_FACE ( 'NONE', ( #87248 ), #106839, .T. ) ;
#6248=CARTESIAN_POINT ( 'NONE',  ( 25.77149322861319547, 20.25929247661551003, 7.808871592221828806 ) ) ;
#6249=VECTOR ( 'NONE', #24832, 1000.000000000000114 ) ;
#6250=LINE ( 'NONE', #17858, #112870 ) ;
#6252=CARTESIAN_POINT ( 'NONE',  ( -22.49999999999984013, 8.319652575858368593, -8.582050562765878965 ) ) ;
#6253=LINE ( 'NONE', #83158, #21269 ) ;
#6254=ORIENTED_EDGE ( 'NONE', *, *, #8560, .T. ) ;
#6256=CARTESIAN_POINT ( 'NONE',  ( 19.62719212111867151, -2.766370489448051195, 4.185522593092497523 ) ) ;
#6257=ORIENTED_EDGE ( 'NONE', *, *, #68273, .T. ) ;
#6258=EDGE_LOOP ( 'NONE', ( #30584, #78388, #115128, #54437 ) ) ;
#6259=ADVANCED_FACE ( 'NONE', ( #10377 ), #97373, .F. ) ;
#6260=EDGE_CURVE ( 'NONE', #1174, #89442, #138319, .T. ) ;
#6262=DIRECTION ( 'NONE',  ( -0.7071067811865487940, 0.7071067811865463515, -0.000000000000000000 ) ) ;
#6263=DIRECTION ( 'NONE',  ( -0.7071067811865486830, -0.7071067811865464625, 0.000000000000000000 ) ) ;
#6266=EDGE_CURVE ( 'NONE', #85257, #83184, #39743, .T. ) ;
#6267=EDGE_CURVE ( 'NONE', #109290, #4040, #28847, .T. ) ;
#6268=CARTESIAN_POINT ( 'NONE',  ( -26.95328719879335821, -22.22500000000000142, 1.979220021349709979 ) ) ;
#6270=AXIS2_PLACEMENT_3D ( 'NONE', #8493, #19414, #64355 ) ;
#6271=EDGE_LOOP ( 'NONE', ( #17812, #77484, #66796, #71598 ) ) ;
#6272=VERTEX_POINT ( 'NONE', #7037 ) ;
#6273=EDGE_CURVE ( 'NONE', #70402, #40720, #73089, .T. ) ;
#6274=ORIENTED_EDGE ( 'NONE', *, *, #47752, .T. ) ;
#6275=VECTOR ( 'NONE', #135418, 1000.000000000000000 ) ;
#6276=DIRECTION ( 'NONE',  ( -0.000000000000000000, 0.3543493200069153248, 0.9351131265310292928 ) ) ;
#6278=EDGE_LOOP ( 'NONE', ( #93735, #76007, #88672, #139863 ) ) ;
#6279=DIRECTION ( 'NONE',  ( -0.7071067811865486830, -0.7071067811865464625, -0.000000000000000000 ) ) ;
#6280=LINE ( 'NONE', #83936, #5495 ) ;
#6281=DIRECTION ( 'NONE',  ( 0.6830127018922180770, -0.6830127018922204085, -0.2588190451025213501 ) ) ;
#6282=AXIS2_PLACEMENT_3D ( 'NONE', #100607, #10691, #24453 ) ;
#6283=DIRECTION ( 'NONE',  ( 0.7071067811865487940, 0.7071067811865463515, 0.000000000000000000 ) ) ;
#6285=ORIENTED_EDGE ( 'NONE', *, *, #113058, .F. ) ;
#6286=LINE ( 'NONE', #15733, #139787 ) ;
#6287=CARTESIAN_POINT ( 'NONE',  ( 51.29974487139158867, -27.71228299555242103, 4.000000000000000000 ) ) ;
#6289=LINE ( 'NONE', #104198, #71388 ) ;
#6290=ORIENTED_EDGE ( 'NONE', *, *, #14014, .F. ) ;
#6292=ORIENTED_EDGE ( 'NONE', *, *, #28839, .T. ) ;
#6293=ORIENTED_EDGE ( 'NONE', *, *, #53671, .F. ) ;
#6295=EDGE_CURVE ( 'NONE', #137809, #3283, #49903, .T. ) ;
#6296=ORIENTED_EDGE ( 'NONE', *, *, #109201, .T. ) ;
#6297=CARTESIAN_POINT ( 'NONE',  ( -30.48921356237309510, -27.52281430457076894, 5.000000000000000000 ) ) ;
#6298=CARTESIAN_POINT ( 'NONE',  ( -31.49999999999977263, 3.052185695429138423, 5.000000000000000000 ) ) ;
#6299=AXIS2_PLACEMENT_3D ( 'NONE', #79846, #99374, #34161 ) ;
#6301=PLANE ( 'NONE',  #121190 ) ;
#6302=EDGE_CURVE ( 'NONE', #6161, #107344, #95509, .T. ) ;
#6303=LINE ( 'NONE', #30996, #127439 ) ;
#6304=CARTESIAN_POINT ( 'NONE',  ( 0.3281693992235254487, -18.74070752338409918, 4.000000000000000000 ) ) ;
#6305=DIRECTION ( 'NONE',  ( -1.000000000000000000, 0.000000000000000000, 0.000000000000000000 ) ) ;
#6307=DIRECTION ( 'NONE',  ( -0.000000000000000000, -0.3543493200069152693, 0.9351131265310292928 ) ) ;
#6308=EDGE_CURVE ( 'NONE', #90006, #132730, #15764, .T. ) ;
#6309=ORIENTED_EDGE ( 'NONE', *, *, #7550, .F. ) ;
#6311=CARTESIAN_POINT ( 'NONE',  ( 26.99999999999980815, 14.58746187583910903, 4.000000000000000000 ) ) ;
#6312=DIRECTION ( 'NONE',  ( 0.7071067811865486830, -0.7071067811865464625, -0.000000000000000000 ) ) ;
#6313=ORIENTED_EDGE ( 'NONE', *, *, #6349, .T. ) ;
#6314=ADVANCED_FACE ( 'NONE', ( #84654 ), #137618, .F. ) ;
#6315=ORIENTED_EDGE ( 'NONE', *, *, #131542, .F. ) ;
#6320=ADVANCED_FACE ( 'NONE', ( #29530 ), #126701, .F. ) ;
#6321=FACE_OUTER_BOUND ( 'NONE', #39398, .T. ) ;
#6323=CARTESIAN_POINT ( 'NONE',  ( -26.99999999999980815, -1.447814304570813393, 5.000000000000000000 ) ) ;
#6326=CARTESIAN_POINT ( 'NONE',  ( 1.499999999999994449, -17.94781430457065241, 5.000000000000000000 ) ) ;
#6327=ORIENTED_EDGE ( 'NONE', *, *, #13694, .T. ) ;
#6329=ORIENTED_EDGE ( 'NONE', *, *, #24203, .T. ) ;
#6332=VECTOR ( 'NONE', #95614, 1000.000000000000000 ) ;
#6335=DIRECTION ( 'NONE',  ( 1.000000000000000000, 0.000000000000000000, 0.000000000000000000 ) ) ;
#6336=ADVANCED_FACE ( 'NONE', ( #11325 ), #133866, .F. ) ;
#6339=ORIENTED_EDGE ( 'NONE', *, *, #22405, .T. ) ;
#6340=ORIENTED_EDGE ( 'NONE', *, *, #44357, .F. ) ;
#6342=CARTESIAN_POINT ( 'NONE',  ( 78.48921356237309510, -27.52281430457109934, 5.000000000000000000 ) ) ;
#6343=VECTOR ( 'NONE', #87446, 1000.000000000000000 ) ;
#6344=LINE ( 'NONE', #10482, #89010 ) ;
#6346=LINE ( 'NONE', #73802, #113062 ) ;
#6347=CARTESIAN_POINT ( 'NONE',  ( -10.49999999999992184, -17.56887692260763956, 4.000000000000000000 ) ) ;
#6348=CARTESIAN_POINT ( 'NONE',  ( 2.292893218813440992, 17.25929247661554200, 5.000000000000000000 ) ) ;
#6349=EDGE_CURVE ( 'NONE', #106517, #141915, #22920, .T. ) ;
#6351=ORIENTED_EDGE ( 'NONE', *, *, #72046, .T. ) ;
#6353=LINE ( 'NONE', #50631, #68533 ) ;
#6354=VERTEX_POINT ( 'NONE', #112294 ) ;
#6355=( BOUNDED_CURVE ( )  B_SPLINE_CURVE ( 3, ( #74740, #8002, #98596, #96423 ),
 .UNSPECIFIED., .F., .T. ) 
 B_SPLINE_CURVE_WITH_KNOTS ( ( 4, 4 ),
 ( 2.779374508378132713, 4.199602562396796301 ),
 .UNSPECIFIED. ) 
 CURVE ( )  GEOMETRIC_REPRESENTATION_ITEM ( )  RATIONAL_B_SPLINE_CURVE ( ( 1.000000000000000000, 0.8388583629366715977, 0.8388583629366715977, 1.000000000000000000 ) ) 
 REPRESENTATION_ITEM ( '' )  );
#6356=DIRECTION ( 'NONE',  ( -0.7071067811865487940, 0.7071067811865463515, -0.000000000000000000 ) ) ;
#6357=CARTESIAN_POINT ( 'NONE',  ( 24.32816939922335209, 8.259292476615634371, 4.000000000000000000 ) ) ;
#6358=ORIENTED_EDGE ( 'NONE', *, *, #32502, .T. ) ;
#6359=EDGE_CURVE ( 'NONE', #55719, #15722, #2045, .T. ) ;
#6360=DIRECTION ( 'NONE',  ( 0.7071067811865486830, -0.7071067811865464625, -0.000000000000000000 ) ) ;
#6361=DIRECTION ( 'NONE',  ( 0.7071067811865486830, -0.7071067811865464625, -0.000000000000000000 ) ) ;
#6362=VECTOR ( 'NONE', #80751, 1000.000000000000000 ) ;
#6363=ORIENTED_EDGE ( 'NONE', *, *, #70716, .F. ) ;
#6365=EDGE_LOOP ( 'NONE', ( #104413, #132437, #110631, #104691 ) ) ;
#6366=DIRECTION ( 'NONE',  ( 0.7071067811865487940, -0.7071067811865463515, 0.000000000000000000 ) ) ;
#6368=VECTOR ( 'NONE', #98548, 999.9999999999998863 ) ;
#6369=PLANE ( 'NONE',  #108681 ) ;
#6370=CARTESIAN_POINT ( 'NONE',  ( 19.49999999999986500, -14.70932175296475108, -11.46312253303841544 ) ) ;
#6371=CARTESIAN_POINT ( 'NONE',  ( -45.18398860626900415, 28.73617430169818832, 5.000000000000000000 ) ) ;
#6372=CARTESIAN_POINT ( 'NONE',  ( 18.28838880452753202, -2.745211937670052560, 5.000000000000000000 ) ) ;
#6373=DIRECTION ( 'NONE',  ( -0.7071067811865486830, 0.7071067811865464625, 0.000000000000000000 ) ) ;
#6376=DIRECTION ( 'NONE',  ( 0.7071067811865486830, -0.7071067811865464625, -0.000000000000000000 ) ) ;
#6377=CARTESIAN_POINT ( 'NONE',  ( -34.45011844616454511, 16.51628081163731210, 5.000000000000000888 ) ) ;
#6378=DIRECTION ( 'NONE',  ( -0.7071067811865487940, 0.7071067811865463515, -0.000000000000000000 ) ) ;
#6379=EDGE_LOOP ( 'NONE', ( #65743, #142958, #61480, #86783 ) ) ;
#6380=EDGE_CURVE ( 'NONE', #140629, #126534, #102133, .T. ) ;
#6381=VERTEX_POINT ( 'NONE', #111560 ) ;
#6383=EDGE_CURVE ( 'NONE', #3235, #28808, #23086, .T. ) ;
#6385=VERTEX_POINT ( 'NONE', #122423 ) ;
#6386=PRODUCT_DEFINITION_SHAPE ( 'NONE', 'NONE',  #114782 ) ;
#6387=DIRECTION ( 'NONE',  ( 0.7071067811865486830, -0.7071067811865464625, -0.000000000000000000 ) ) ;
#6388=DIRECTION ( 'NONE',  ( -0.7071067811865486830, -0.7071067811865464625, -0.000000000000000000 ) ) ;
#6389=DIRECTION ( 'NONE',  ( 1.000000000000000000, 0.000000000000000000, 0.000000000000000000 ) ) ;
#6390=ORIENTED_EDGE ( 'NONE', *, *, #94489, .F. ) ;
#6391=CARTESIAN_POINT ( 'NONE',  ( 65.99451991528749772, 28.92564299267984396, 4.000000000000000000 ) ) ;
#6393=DIRECTION ( 'NONE',  ( -0.3543493200069162685, -0.000000000000000000, -0.9351131265310288487 ) ) ;
#6394=DIRECTION ( 'NONE',  ( -0.7071067811865486830, -0.7071067811865464625, 0.000000000000000000 ) ) ;
#6395=ADVANCED_FACE ( 'NONE', ( #67368 ), #113705, .T. ) ;
#6396=CARTESIAN_POINT ( 'NONE',  ( -48.48921356237309510, -27.52281430457089328, 5.000000000000000000 ) ) ;
#6397=CARTESIAN_POINT ( 'NONE',  ( -20.20710678118640047, 9.759292476615620160, 5.000000000000000000 ) ) ;
#6399=FACE_OUTER_BOUND ( 'NONE', #95298, .T. ) ;
#6400=DIRECTION ( 'NONE',  ( -0.6830127018922180770, -0.6830127018922204085, -0.2588190451025213501 ) ) ;
#6401=DIRECTION ( 'NONE',  ( -0.000000000000000000, 0.3543493200069152138, -0.9351131265310292928 ) ) ;
#6402=LINE ( 'NONE', #50682, #114722 ) ;
#6403=CARTESIAN_POINT ( 'NONE',  ( 33.32816939922330590, 8.259292476615641476, 4.000000000000000000 ) ) ;
#6404=EDGE_LOOP ( 'NONE', ( #63848, #56010, #39368, #102203 ) ) ;
#6405=ORIENTED_EDGE ( 'NONE', *, *, #113080, .F. ) ;
#6407=VECTOR ( 'NONE', #8272, 1000.000000000000000 ) ;
#6408=EDGE_LOOP ( 'NONE', ( #84459, #11315, #37532, #89468 ) ) ;
#6410=LINE ( 'NONE', #118793, #103326 ) ;
#6411=ORIENTED_EDGE ( 'NONE', *, *, #11682, .F. ) ;
#6412=DIRECTION ( 'NONE',  ( -0.6830127018922180770, -0.6830127018922204085, -0.2588190451025213501 ) ) ;
#6413=CARTESIAN_POINT ( 'NONE',  ( 0.000000000000000000, 0.000000000000000000, 5.000000000000000000 ) ) ;
#6414=AXIS2_PLACEMENT_3D ( 'NONE', #119813, #131446, #53908 ) ;
#6416=ORIENTED_EDGE ( 'NONE', *, *, #114822, .T. ) ;
#6418=VERTEX_POINT ( 'NONE', #56525 ) ;
#6419=DIRECTION ( 'NONE',  ( 0.7071067811865486830, -0.7071067811865464625, -0.000000000000000000 ) ) ;
#6420=LINE ( 'NONE', #50007, #42585 ) ;
#6421=DIRECTION ( 'NONE',  ( 0.6830127018922180770, -0.6830127018922204085, -0.2588190451025213501 ) ) ;
#6422=VECTOR ( 'NONE', #67943, 1000.000000000000227 ) ;
#6423=CARTESIAN_POINT ( 'NONE',  ( 16.49999999999988631, -8.568876922607721269, 4.000000000000000000 ) ) ;
#6424=EDGE_CURVE ( 'NONE', #46535, #89080, #23850, .T. ) ;
#6425=EDGE_LOOP ( 'NONE', ( #110653, #55389, #64217, #42236 ) ) ;
#6426=ORIENTED_EDGE ( 'NONE', *, *, #54087, .F. ) ;
#6428=ORIENTED_EDGE ( 'NONE', *, *, #119260, .T. ) ;
#6429=CARTESIAN_POINT ( 'NONE',  ( -32.57672154193627279, 11.25929247661560240, 17.85071094206591980 ) ) ;
#6430=EDGE_CURVE ( 'NONE', #106470, #130798, #325, .T. ) ;
#6433=VECTOR ( 'NONE', #116188, 1000.000000000000000 ) ;
#6434=AXIS2_PLACEMENT_3D ( 'NONE', #115071, #112965, #112273 ) ;
#6435=LINE ( 'NONE', #138445, #140581 ) ;
#6436=EDGE_CURVE ( 'NONE', #10426, #23231, #46351, .T. ) ;
#6437=ADVANCED_FACE ( 'NONE', ( #135482 ), #58676, .F. ) ;
#6438=ADVANCED_FACE ( 'NONE', ( #15087 ), #3485, .F. ) ;
#6440=EDGE_LOOP ( 'NONE', ( #110970, #142495, #99455, #102318 ) ) ;
#6441=FACE_OUTER_BOUND ( 'NONE', #125490, .T. ) ;
#6442=EDGE_CURVE ( 'NONE', #118295, #83675, #136168, .T. ) ;
#6443=ORIENTED_EDGE ( 'NONE', *, *, #126478, .F. ) ;
#6444=ORIENTED_EDGE ( 'NONE', *, *, #60436, .F. ) ;
#6445=ADVANCED_FACE ( 'NONE', ( #89802 ), #103517, .F. ) ;
#6447=EDGE_CURVE ( 'NONE', #106060, #117536, #137084, .T. ) ;
#6448=DIRECTION ( 'NONE',  ( -0.000000000000000000, 0.000000000000000000, 1.000000000000000000 ) ) ;
#6449=LINE ( 'NONE', #50027, #77323 ) ;
#6450=VERTEX_POINT ( 'NONE', #34930 ) ;
#6452=LINE ( 'NONE', #84106, #22353 ) ;
#6453=DIRECTION ( 'NONE',  ( 0.7071067811865486830, -0.7071067811865464625, -0.000000000000000000 ) ) ;
#6455=VERTEX_POINT ( 'NONE', #78424 ) ;
#6456=VECTOR ( 'NONE', #72795, 1000.000000000000227 ) ;
#6457=EDGE_CURVE ( 'NONE', #26438, #32517, #13840, .T. ) ;
#6458=CARTESIAN_POINT ( 'NONE',  ( 14.17270155891586825, -22.22500000000000142, -13.60495448913695249 ) ) ;
#6460=VERTEX_POINT ( 'NONE', #24741 ) ;
#6461=CARTESIAN_POINT ( 'NONE',  ( -20.99451991528748707, 28.92564299267952777, 4.000000000000000000 ) ) ;
#6464=ORIENTED_EDGE ( 'NONE', *, *, #61025, .F. ) ;
#6465=DIRECTION ( 'NONE',  ( -0.3543493200069163240, -0.000000000000000000, 0.9351131265310288487 ) ) ;
#6466=VERTEX_POINT ( 'NONE', #134970 ) ;
#6467=VECTOR ( 'NONE', #96359, 1000.000000000000000 ) ;
#6468=EDGE_LOOP ( 'NONE', ( #91660, #91671, #2360, #143260 ) ) ;
#6469=EDGE_CURVE ( 'NONE', #126032, #12409, #68299, .T. ) ;
#6470=EDGE_LOOP ( 'NONE', ( #136519, #119054, #125253, #118105 ) ) ;
#6471=LINE ( 'NONE', #117400, #41800 ) ;
#6472=CARTESIAN_POINT ( 'NONE',  ( 34.75611968250419181, 10.70565069852394302, 4.955485411084881164 ) ) ;
#6473=LINE ( 'NONE', #41286, #33355 ) ;
#6474=PLANE ( 'NONE',  #34631 ) ;
#6475=CARTESIAN_POINT ( 'NONE',  ( 63.29974487139158867, -27.71228299555250274, 4.000000000000000000 ) ) ;
#6476=FACE_OUTER_BOUND ( 'NONE', #63877, .T. ) ;
#6477=LINE ( 'NONE', #139931, #45878 ) ;
#6478=DIRECTION ( 'NONE',  ( -0.7071067811865486830, 0.7071067811865464625, 0.000000000000000000 ) ) ;
#6479=AXIS2_PLACEMENT_3D ( 'NONE', #139930, #7938, #86249 ) ;
#6480=CARTESIAN_POINT ( 'NONE',  ( 5.292893218813421896, 20.25929247661551713, 5.000000000000000000 ) ) ;
#6481=VECTOR ( 'NONE', #103377, 1000.000000000000000 ) ;
#6483=DIRECTION ( 'NONE',  ( 0.7071067811865487940, 0.7071067811865463515, 0.000000000000000000 ) ) ;
#6484=CARTESIAN_POINT ( 'NONE',  ( 39.18398860626899705, 28.73617430169814568, 5.000000000000000000 ) ) ;
#6486=EDGE_CURVE ( 'NONE', #71266, #17986, #111765, .T. ) ;
#6487=ORIENTED_EDGE ( 'NONE', *, *, #81182, .F. ) ;
#6488=VERTEX_POINT ( 'NONE', #103701 ) ;
#6489=VERTEX_POINT ( 'NONE', #56714 ) ;
#6491=VERTEX_POINT ( 'NONE', #79172 ) ;
#6492=EDGE_CURVE ( 'NONE', #31789, #27164, #23293, .T. ) ;
#6493=ORIENTED_EDGE ( 'NONE', *, *, #42727, .F. ) ;
#6494=CARTESIAN_POINT ( 'NONE',  ( -6.328169399223487090, -9.740707523384186217, 4.000000000000000000 ) ) ;
#6495=LINE ( 'NONE', #93567, #94267 ) ;
#6496=LINE ( 'NONE', #73258, #131904 ) ;
#6497=ORIENTED_EDGE ( 'NONE', *, *, #50851, .T. ) ;
#6498=FACE_OUTER_BOUND ( 'NONE', #38814, .T. ) ;
#6499=VERTEX_POINT ( 'NONE', #125499 ) ;
#6500=EDGE_CURVE ( 'NONE', #82848, #44234, #113896, .T. ) ;
#6502=FACE_OUTER_BOUND ( 'NONE', #112165, .T. ) ;
#6504=ORIENTED_EDGE ( 'NONE', *, *, #71864, .T. ) ;
#6507=LINE ( 'NONE', #73969, #118426 ) ;
#6508=EDGE_CURVE ( 'NONE', #78770, #9427, #2242, .T. ) ;
#6509=DIRECTION ( 'NONE',  ( -0.000000000000000000, -0.3543493200069152693, 0.9351131265310292928 ) ) ;
#6510=ORIENTED_EDGE ( 'NONE', *, *, #72524, .F. ) ;
#6511=ORIENTED_EDGE ( 'NONE', *, *, #85915, .F. ) ;
#6512=CARTESIAN_POINT ( 'NONE',  ( -39.18398860626899705, 28.73617430169814568, 5.000000000000000000 ) ) ;
#6517=ORIENTED_EDGE ( 'NONE', *, *, #53098, .F. ) ;
#6518=DIRECTION ( 'NONE',  ( -0.3543493200069162685, -0.000000000000000000, -0.9351131265310288487 ) ) ;
#6519=DIRECTION ( 'NONE',  ( -0.3543493200069162685, -0.000000000000000000, -0.9351131265310288487 ) ) ;
#6520=DIRECTION ( 'NONE',  ( -0.6830127018922181881, 0.6830127018922202975, -0.2588190451025214056 ) ) ;
#6521=VERTEX_POINT ( 'NONE', #69713 ) ;
#6526=ORIENTED_EDGE ( 'NONE', *, *, #116222, .T. ) ;
#6527=AXIS2_PLACEMENT_3D ( 'NONE', #26477, #69283, #23615 ) ;
#6528=PLANE ( 'NONE',  #32457 ) ;
#6529=VERTEX_POINT ( 'NONE', #58137 ) ;
#6530=ADVANCED_FACE ( 'NONE', ( #100875 ), #123376, .T. ) ;
#6531=VECTOR ( 'NONE', #119413, 1000.000000000000000 ) ;
#6533=ORIENTED_EDGE ( 'NONE', *, *, #58883, .F. ) ;
#6535=CARTESIAN_POINT ( 'NONE',  ( -14.81601139373099585, 28.73617430169776910, 5.000000000000000000 ) ) ;
#6537=VERTEX_POINT ( 'NONE', #103026 ) ;
#6538=DIRECTION ( 'NONE',  ( -0.7071067811865486830, 0.7071067811865464625, 0.000000000000000000 ) ) ;
#6539=CIRCLE ( 'NONE', #133986, 5.968999999999998529 ) ;
#6540=( BOUNDED_CURVE ( )  B_SPLINE_CURVE ( 3, ( #51410, #71742, #60154, #104319 ),
 .UNSPECIFIED., .F., .T. ) 
 B_SPLINE_CURVE_WITH_KNOTS ( ( 4, 4 ),
 ( 1.964434688349485869, 3.503810798801452187 ),
 .UNSPECIFIED. ) 
 CURVE ( )  GEOMETRIC_REPRESENTATION_ITEM ( )  RATIONAL_B_SPLINE_CURVE ( ( 1.000000000000000000, 0.8120851936182275077, 0.8120851936182275077, 1.000000000000000000 ) ) 
 REPRESENTATION_ITEM ( '' )  );
#6541=CARTESIAN_POINT ( 'NONE',  ( 21.79289321881331176, -17.24070752338410628, 5.000000000000000000 ) ) ;
#6542=CARTESIAN_POINT ( 'NONE',  ( 9.792893218813397027, 9.759292476615621936, 5.000000000000000000 ) ) ;
#6543=CARTESIAN_POINT ( 'NONE',  ( -12.48921356237309155, -27.52281430457064104, 5.000000000000000000 ) ) ;
#6544=CARTESIAN_POINT ( 'NONE',  ( 19.35824297541128303, 15.75929247661556332, 19.34181609438695304 ) ) ;
#6546=LINE ( 'NONE', #61723, #51720 ) ;
#6547=CARTESIAN_POINT ( 'NONE',  ( 15.18398860626900237, 28.73617430169797871, 5.000000000000000000 ) ) ;
#6548=FACE_OUTER_BOUND ( 'NONE', #41963, .T. ) ;
#6549=VECTOR ( 'NONE', #105351, 1000.000000000000000 ) ;
#6550=DIRECTION ( 'NONE',  ( 0.7071067811865487940, 0.7071067811865463515, 0.000000000000000000 ) ) ;
#6551=CARTESIAN_POINT ( 'NONE',  ( -34.49999999999975131, -10.91253812416064228, 4.000000000000000000 ) ) ;
#6552=FACE_OUTER_BOUND ( 'NONE', #50547, .T. ) ;
#6553=ORIENTED_EDGE ( 'NONE', *, *, #107751, .T. ) ;
#6554=EDGE_CURVE ( 'NONE', #10831, #24144, #47276, .T. ) ;
#6556=ORIENTED_EDGE ( 'NONE', *, *, #25142, .F. ) ;
#6558=VECTOR ( 'NONE', #96959, 1000.000000000000000 ) ;
#6559=ADVANCED_FACE ( 'NONE', ( #47962 ), #3665, .T. ) ;
#6563=CARTESIAN_POINT ( 'NONE',  ( -21.18398860626899349, 28.73617430169802134, 5.000000000000000000 ) ) ;
#6564=AXIS2_PLACEMENT_3D ( 'NONE', #35541, #11567, #81163 ) ;
#6565=DIRECTION ( 'NONE',  ( -0.7071067811865487940, 0.7071067811865463515, -0.000000000000000000 ) ) ;
#6566=VERTEX_POINT ( 'NONE', #115275 ) ;
#6567=DIRECTION ( 'NONE',  ( 0.6830127018922180770, -0.6830127018922204085, -0.2588190451025213501 ) ) ;
#6568=VECTOR ( 'NONE', #90022, 999.9999999999998863 ) ;
#6569=CARTESIAN_POINT ( 'NONE',  ( 6.183988606268994381, 28.73617430169791476, 5.000000000000000000 ) ) ;
#6570=VECTOR ( 'NONE', #135479, 1000.000000000000227 ) ;
#6572=LINE ( 'NONE', #30534, #113753 ) ;
#6574=VERTEX_POINT ( 'NONE', #116748 ) ;
#6575=EDGE_CURVE ( 'NONE', #25422, #129576, #82027, .T. ) ;
#6576=LINE ( 'NONE', #4409, #144 ) ;
#6577=FACE_OUTER_BOUND ( 'NONE', #128170, .T. ) ;
#6578=CARTESIAN_POINT ( 'NONE',  ( -30.18398860626900060, 28.73617430169808173, 5.000000000000000000 ) ) ;
#6581=DIRECTION ( 'NONE',  ( -0.7071067811865486830, -0.7071067811865464625, 0.000000000000000000 ) ) ;
#6584=CARTESIAN_POINT ( 'NONE',  ( -45.18398860626900415, 28.73617430169818832, 5.000000000000000000 ) ) ;
#6586=ORIENTED_EDGE ( 'NONE', *, *, #98632, .F. ) ;
#6589=ORIENTED_EDGE ( 'NONE', *, *, #113692, .T. ) ;
#6590=CARTESIAN_POINT ( 'NONE',  ( -45.48921356237309510, -27.52281430457087197, 5.000000000000000000 ) ) ;
#6591=DIRECTION ( 'NONE',  ( 0.7071067811865487940, -0.7071067811865463515, 0.000000000000000000 ) ) ;
#6592=VECTOR ( 'NONE', #88065, 999.9999999999998863 ) ;
#6593=CARTESIAN_POINT ( 'NONE',  ( 4.499999999999968914, 3.653845994658392993, -4.504631822206380143 ) ) ;
#6594=VECTOR ( 'NONE', #34246, 1000.000000000000000 ) ;
#6597=ORIENTED_EDGE ( 'NONE', *, *, #51752, .T. ) ;
#6598=DIRECTION ( 'NONE',  ( 0.7071067811865486830, -0.7071067811865464625, -0.000000000000000000 ) ) ;
#6599=VERTEX_POINT ( 'NONE', #71850 ) ;
#6600=DIRECTION ( 'NONE',  ( 0.6830127018922180770, -0.6830127018922204085, -0.2588190451025213501 ) ) ;
#6601=DIRECTION ( 'NONE',  ( -0.3543493200069162685, -0.000000000000000000, -0.9351131265310288487 ) ) ;
#6602=FACE_OUTER_BOUND ( 'NONE', #109818, .T. ) ;
#6603=LINE ( 'NONE', #50888, #69652 ) ;
#6604=ORIENTED_EDGE ( 'NONE', *, *, #136946, .F. ) ;
#6608=PLANE ( 'NONE',  #136474 ) ;
#6609=DIRECTION ( 'NONE',  ( 0.7071067811865486830, -0.7071067811865464625, -0.000000000000000000 ) ) ;
#6610=FACE_OUTER_BOUND ( 'NONE', #16587, .T. ) ;
#6611=ADVANCED_FACE ( 'NONE', ( #126206 ), #82709, .F. ) ;
#6613=EDGE_CURVE ( 'NONE', #82440, #101030, #26883, .T. ) ;
#6614=VERTEX_POINT ( 'NONE', #5094 ) ;
#6615=EDGE_CURVE ( 'NONE', #51943, #113850, #15965, .T. ) ;
#6616=DIRECTION ( 'NONE',  ( -0.000000000000000000, 0.000000000000000000, 1.000000000000000000 ) ) ;
#6618=EDGE_CURVE ( 'NONE', #55005, #127158, #137811, .T. ) ;
#6619=ORIENTED_EDGE ( 'NONE', *, *, #9325, .T. ) ;
#6620=VERTEX_POINT ( 'NONE', #50086 ) ;
#6621=CARTESIAN_POINT ( 'NONE',  ( 34.92499999999998295, 16.81783344222320764, 7.048977539241891854 ) ) ;
#6622=ORIENTED_EDGE ( 'NONE', *, *, #60220, .F. ) ;
#6623=EDGE_CURVE ( 'NONE', #138876, #106778, #38486, .T. ) ;
#6624=CARTESIAN_POINT ( 'NONE',  ( -28.49999999999980460, -19.53360074219753884, 5.000000000000000000 ) ) ;
#6625=ORIENTED_EDGE ( 'NONE', *, *, #98170, .T. ) ;
#6626=CARTESIAN_POINT ( 'NONE',  ( 9.489213562373095101, -27.52281430457062328, 5.000000000000000000 ) ) ;
#6627=ADVANCED_FACE ( 'NONE', ( #72593 ), #127639, .F. ) ;
#6628=VECTOR ( 'NONE', #90314, 1000.000000000000227 ) ;
#6629=VECTOR ( 'NONE', #62057, 999.9999999999998863 ) ;
#6630=AXIS2_PLACEMENT_3D ( 'NONE', #2177, #114543, #45765 ) ;
#6631=LINE ( 'NONE', #117554, #85859 ) ;
#6632=AXIS2_PLACEMENT_3D ( 'NONE', #113117, #13782, #25387 ) ;
#6634=FACE_BOUND ( 'NONE', #127900, .T. ) ;
#6635=EDGE_CURVE ( 'NONE', #17037, #64792, #23450, .T. ) ;
#6636=CARTESIAN_POINT ( 'NONE',  ( -8.816011393731004731, 28.73617430169781173, 5.000000000000000000 ) ) ;
#6637=CARTESIAN_POINT ( 'NONE',  ( -1.499999999999980460, 10.46639925780215918, 5.000000000000000000 ) ) ;
#6638=CARTESIAN_POINT ( 'NONE',  ( 33.32816939922329880, -9.740707523384177335, 4.000000000000000000 ) ) ;
#6639=ORIENTED_EDGE ( 'NONE', *, *, #88874, .T. ) ;
#6640=DIRECTION ( 'NONE',  ( 0.6830127018922180770, -0.6830127018922204085, -0.2588190451025213501 ) ) ;
#6641=LINE ( 'NONE', #127029, #1870 ) ;
#6642=ORIENTED_EDGE ( 'NONE', *, *, #72988, .T. ) ;
#6645=VECTOR ( 'NONE', #107082, 1000.000000000000000 ) ;
#6646=CARTESIAN_POINT ( 'NONE',  ( 60.48921356237309510, -27.52281430457097500, 5.000000000000000000 ) ) ;
#6647=EDGE_CURVE ( 'NONE', #29058, #68553, #54680, .T. ) ;
#6648=EDGE_LOOP ( 'NONE', ( #32639, #99634, #24726, #73212 ) ) ;
#6650=EDGE_LOOP ( 'NONE', ( #43418, #19939, #55018, #7695 ) ) ;
#6651=CARTESIAN_POINT ( 'NONE',  ( -34.42500000000001137, -22.22500000000000142, 5.000000000000000000 ) ) ;
#6652=DIRECTION ( 'NONE',  ( 0.7071067811865487940, -0.7071067811865463515, 0.000000000000000000 ) ) ;
#6653=ORIENTED_EDGE ( 'NONE', *, *, #23459, .T. ) ;
#6655=AXIS2_PLACEMENT_3D ( 'NONE', #96417, #41345, #76139 ) ;
#6658=CARTESIAN_POINT ( 'NONE',  ( 18.42327845806342879, 11.25929247661560240, 17.85071094206580256 ) ) ;
#6659=DIRECTION ( 'NONE',  ( -0.7071067811865486830, -0.7071067811865464625, 0.000000000000000000 ) ) ;
#6660=CARTESIAN_POINT ( 'NONE',  ( 17.99999999999987566, -12.03360074219761700, 5.000000000000000000 ) ) ;
#6661=CARTESIAN_POINT ( 'NONE',  ( -24.18398860626899705, 28.73617430169804265, 5.000000000000000000 ) ) ;
#6662=ORIENTED_EDGE ( 'NONE', *, *, #35406, .F. ) ;
#6663=ADVANCED_FACE ( 'NONE', ( #78568 ), #65581, .F. ) ;
#6665=VECTOR ( 'NONE', #18384, 1000.000000000000000 ) ;
#6667=FACE_OUTER_BOUND ( 'NONE', #57202, .T. ) ;
#6668=EDGE_LOOP ( 'NONE', ( #70299, #40983, #25379, #68741 ) ) ;
#6672=ORIENTED_EDGE ( 'NONE', *, *, #41107, .T. ) ;
#6673=PLANE ( 'NONE',  #46714 ) ;
#6675=DIRECTION ( 'NONE',  ( 0.7071067811865487940, 0.7071067811865463515, 0.000000000000000000 ) ) ;
#6676=VERTEX_POINT ( 'NONE', #10422 ) ;
#6677=VECTOR ( 'NONE', #50493, 1000.000000000000000 ) ;
#6678=DIRECTION ( 'NONE',  ( -0.6830127018922181881, 0.6830127018922202975, -0.2588190451025214056 ) ) ;
#6679=VECTOR ( 'NONE', #117401, 999.9999999999998863 ) ;
#6680=EDGE_CURVE ( 'NONE', #115089, #82492, #122034, .T. ) ;
#6681=CARTESIAN_POINT ( 'NONE',  ( -4.828169399223497749, -17.24070752338410273, 4.000000000000000000 ) ) ;
#6683=CARTESIAN_POINT ( 'NONE',  ( -23.99999999999982947, -4.447814304570784749, 5.000000000000000000 ) ) ;
#6685=CARTESIAN_POINT ( 'NONE',  ( 22.19018167574434486, -18.74070752338409207, 7.910009926591455631 ) ) ;
#6686=CARTESIAN_POINT ( 'NONE',  ( 23.20666063542136115, 21.75929247661548871, 4.998822639870701856 ) ) ;
#6687=EDGE_CURVE ( 'NONE', #87956, #115779, #11116, .T. ) ;
#6688=DIRECTION ( 'NONE',  ( -0.000000000000000000, 0.000000000000000000, 1.000000000000000000 ) ) ;
#6689=VECTOR ( 'NONE', #64456, 1000.000000000000000 ) ;
#6690=LINE ( 'NONE', #60441, #26366 ) ;
#6691=ORIENTED_EDGE ( 'NONE', *, *, #92956, .T. ) ;
#6692=DIRECTION ( 'NONE',  ( -0.000000000000000000, 0.000000000000000000, 1.000000000000000000 ) ) ;
#6693=ORIENTED_EDGE ( 'NONE', *, *, #8978, .T. ) ;
#6694=DIRECTION ( 'NONE',  ( -0.000000000000000000, 0.000000000000000000, 1.000000000000000000 ) ) ;
#6695=FACE_OUTER_BOUND ( 'NONE', #75409, .T. ) ;
#6696=CARTESIAN_POINT ( 'NONE',  ( -27.18398860626900060, 28.73617430169806042, 5.000000000000000000 ) ) ;
#6697=ORIENTED_EDGE ( 'NONE', *, *, #132137, .T. ) ;
#6698=EDGE_CURVE ( 'NONE', #97116, #36198, #45255, .T. ) ;
#6699=DIRECTION ( 'NONE',  ( -0.7071067811865486830, -0.7071067811865464625, 0.000000000000000000 ) ) ;
#6700=DIRECTION ( 'NONE',  ( 0.3543493200069162685, -0.000000000000000000, -0.9351131265310288487 ) ) ;
#6701=DIRECTION ( 'NONE',  ( -0.000000000000000000, 0.3543493200069153248, 0.9351131265310292928 ) ) ;
#6702=EDGE_LOOP ( 'NONE', ( #74959, #86419, #30724, #30274 ) ) ;
#6703=DIRECTION ( 'NONE',  ( 1.000000000000000000, 0.000000000000000000, 0.000000000000000000 ) ) ;
#6704=DIRECTION ( 'NONE',  ( 0.6830127018922181881, 0.6830127018922202975, -0.2588190451025214056 ) ) ;
#6705=PLANE ( 'NONE',  #139568 ) ;
#6706=CARTESIAN_POINT ( 'NONE',  ( -26.81601139373100651, 28.73617430169768738, 5.000000000000000000 ) ) ;
#6707=DIRECTION ( 'NONE',  ( 0.6830127018922181881, 0.6830127018922202975, -0.2588190451025214056 ) ) ;
#6710=ORIENTED_EDGE ( 'NONE', *, *, #32929, .T. ) ;
#6711=CARTESIAN_POINT ( 'NONE',  ( 27.18398860626900060, 28.73617430169806042, 5.000000000000000000 ) ) ;
#6714=CARTESIAN_POINT ( 'NONE',  ( -54.48921356237310221, -27.52281430457093236, 5.000000000000000000 ) ) ;
#6715=CARTESIAN_POINT ( 'NONE',  ( -33.70710678118630454, 11.25929247661560417, 5.000000000000000000 ) ) ;
#6716=PLANE ( 'NONE',  #12024 ) ;
#6717=ORIENTED_EDGE ( 'NONE', *, *, #83126, .F. ) ;
#6718=LINE ( 'NONE', #139468, #74310 ) ;
#6719=LINE ( 'NONE', #136033, #132296 ) ;
#6720=DIRECTION ( 'NONE',  ( 0.7071067811865487940, 0.7071067811865463515, -0.000000000000000000 ) ) ;
#6721=DIRECTION ( 'NONE',  ( 1.000000000000000000, 0.000000000000000000, 0.000000000000000000 ) ) ;
#6723=DIRECTION ( 'NONE',  ( 0.6830127018922180770, -0.6830127018922204085, -0.2588190451025213501 ) ) ;
#6724=ORIENTED_EDGE ( 'NONE', *, *, #119414, .T. ) ;
#6725=LINE ( 'NONE', #20486, #99640 ) ;
#6726=ADVANCED_FACE ( 'NONE', ( #121334 ), #12570, .F. ) ;
#6727=ORIENTED_EDGE ( 'NONE', *, *, #135802, .F. ) ;
#6728=EDGE_CURVE ( 'NONE', #91342, #126947, #111153, .T. ) ;
#6730=CARTESIAN_POINT ( 'NONE',  ( -27.29974487139158512, -27.71228299555225405, 4.000000000000000000 ) ) ;
#6733=VECTOR ( 'NONE', #138068, 1000.000000000000000 ) ;
#6734=CARTESIAN_POINT ( 'NONE',  ( 0.3281693992235254487, -15.74070752338412760, 4.000000000000000000 ) ) ;
#6735=CARTESIAN_POINT ( 'NONE',  ( -38.38161509397980353, -2.240707523384260824, 13.37739548510248255 ) ) ;
#6736=VECTOR ( 'NONE', #116530, 1000.000000000000000 ) ;
#6737=CARTESIAN_POINT ( 'NONE',  ( 2.999999999999988898, -13.44781430457069682, 5.000000000000000000 ) ) ;
#6738=EDGE_CURVE ( 'NONE', #97151, #75676, #99566, .T. ) ;
#6739=FACE_OUTER_BOUND ( 'NONE', #101837, .T. ) ;
#6740=ORIENTED_EDGE ( 'NONE', *, *, #4687, .F. ) ;
#6742=DIRECTION ( 'NONE',  ( -0.7071067811865486830, -0.7071067811865464625, -0.000000000000000000 ) ) ;
#6743=DIRECTION ( 'NONE',  ( -0.3543493200069162685, -0.000000000000000000, -0.9351131265310288487 ) ) ;
#6744=DIRECTION ( 'NONE',  ( -0.3543493200069162685, -0.000000000000000000, -0.9351131265310288487 ) ) ;
#6745=AXIS2_PLACEMENT_3D ( 'NONE', #56016, #80608, #124806 ) ;
#6747=CARTESIAN_POINT ( 'NONE',  ( 14.99451991528749595, 28.92564299267948513, 4.000000000000000000 ) ) ;
#6748=LINE ( 'NONE', #51029, #27258 ) ;
#6750=CARTESIAN_POINT ( 'NONE',  ( 0.000000000000000000, 0.000000000000000000, 5.000000000000000000 ) ) ;
#6751=ORIENTED_EDGE ( 'NONE', *, *, #96871, .F. ) ;
#6752=ORIENTED_EDGE ( 'NONE', *, *, #29268, .T. ) ;
#6754=CARTESIAN_POINT ( 'NONE',  ( -68.99451991528748351, 28.92564299267986172, 4.000000000000000000 ) ) ;
#6755=LINE ( 'NONE', #83691, #83317 ) ;
#6757=VECTOR ( 'NONE', #66321, 1000.000000000000000 ) ;
#6759=ORIENTED_EDGE ( 'NONE', *, *, #117336, .T. ) ;
#6760=EDGE_CURVE ( 'NONE', #61260, #85411, #6823, .T. ) ;
#6761=( BOUNDED_CURVE ( )  B_SPLINE_CURVE ( 3, ( #23227, #79106, #77658, #64619 ),
 .UNSPECIFIED., .F., .F. ) 
 B_SPLINE_CURVE_WITH_KNOTS ( ( 4, 4 ),
 ( 1.964434688349486979, 3.503810798801452187 ),
 .UNSPECIFIED. ) 
 CURVE ( )  GEOMETRIC_REPRESENTATION_ITEM ( )  RATIONAL_B_SPLINE_CURVE ( ( 1.000000000000000000, 0.8120851936182278408, 0.8120851936182278408, 1.000000000000000000 ) ) 
 REPRESENTATION_ITEM ( '' )  );
#6762=LINE ( 'NONE', #95239, #58373 ) ;
#6763=AXIS2_PLACEMENT_3D ( 'NONE', #6750, #16973, #94507 ) ;
#6765=VERTEX_POINT ( 'NONE', #31489 ) ;
#6766=LINE ( 'NONE', #106826, #126530 ) ;
#6769=DIRECTION ( 'NONE',  ( -0.6830127018922181881, 0.6830127018922202975, -0.2588190451025214056 ) ) ;
#6772=DIRECTION ( 'NONE',  ( -0.000000000000000000, -0.3543493200069152693, 0.9351131265310292928 ) ) ;
#6773=DIRECTION ( 'NONE',  ( 0.7071067811865486830, -0.7071067811865464625, -0.000000000000000000 ) ) ;
#6774=VECTOR ( 'NONE', #126244, 1000.000000000000000 ) ;
#6776=CARTESIAN_POINT ( 'NONE',  ( 44.99451991528749772, 28.92564299267969474, 4.000000000000000000 ) ) ;
#6777=DIRECTION ( 'NONE',  ( -0.000000000000000000, -0.3543493200069152693, 0.9351131265310292928 ) ) ;
#6779=AXIS2_PLACEMENT_3D ( 'NONE', #137329, #104677, #19098 ) ;
#6781=CARTESIAN_POINT ( 'NONE',  ( -29.20666063542132207, 21.75929247661549226, 4.998822639870711626 ) ) ;
#6782=DIRECTION ( 'NONE',  ( 0.7071067811865487940, 0.7071067811865463515, 0.000000000000000000 ) ) ;
#6783=VECTOR ( 'NONE', #136771, 1000.000000000000227 ) ;
#6784=CARTESIAN_POINT ( 'NONE',  ( 23.99999999999983658, 7.552185695429090906, 5.000000000000000000 ) ) ;
#6785=CARTESIAN_POINT ( 'NONE',  ( 16.49999999999988276, -4.216083040037233332, -7.486842126848696211 ) ) ;
#6786=VECTOR ( 'NONE', #76288, 999.9999999999998863 ) ;
#6787=EDGE_LOOP ( 'NONE', ( #84850, #67843, #87072, #134403 ) ) ;
#6788=EDGE_CURVE ( 'NONE', #39740, #42277, #108283, .T. ) ;
#6792=EDGE_CURVE ( 'NONE', #1646, #63895, #109020, .T. ) ;
#6793=DIRECTION ( 'NONE',  ( -0.6830127018922180770, 0.6830127018922202975, -0.2588190451025213501 ) ) ;
#6794=LINE ( 'NONE', #135927, #27118 ) ;
#6795=CARTESIAN_POINT ( 'NONE',  ( 29.28242261357413057, -21.73023691814492864, 5.000000000000000888 ) ) ;
#6796=FACE_OUTER_BOUND ( 'NONE', #143496, .T. ) ;
#6797=EDGE_LOOP ( 'NONE', ( #15955, #70142, #26620, #15043 ) ) ;
#6798=ORIENTED_EDGE ( 'NONE', *, *, #18450, .T. ) ;
#6800=CARTESIAN_POINT ( 'NONE',  ( 30.72281430457039875, -21.72499999999999432, 5.000000000000000000 ) ) ;
#6802=ORIENTED_EDGE ( 'NONE', *, *, #57956, .F. ) ;
#6803=EDGE_CURVE ( 'NONE', #111332, #9354, #95010, .T. ) ;
#6804=ADVANCED_FACE ( 'NONE', ( #19875 ), #40248, .F. ) ;
#6805=ORIENTED_EDGE ( 'NONE', *, *, #51882, .T. ) ;
#6806=LINE ( 'NONE', #50368, #139402 ) ;
#6807=ORIENTED_EDGE ( 'NONE', *, *, #125783, .F. ) ;
#6809=ADVANCED_FACE ( 'NONE', ( #86596 ), #119881, .T. ) ;
#6810=FACE_BOUND ( 'NONE', #33951, .T. ) ;
#6811=EDGE_CURVE ( 'NONE', #18156, #68806, #76431, .T. ) ;
#6812=PLANE ( 'NONE',  #80382 ) ;
#6813=PLANE ( 'NONE',  #11928 ) ;
#6815=CARTESIAN_POINT ( 'NONE',  ( 44.99451991528749772, 28.92564299267969474, 4.000000000000000000 ) ) ;
#6816=VERTEX_POINT ( 'NONE', #7564 ) ;
#6817=CARTESIAN_POINT ( 'NONE',  ( -3.489213562373097322, -27.52281430457057709, 5.000000000000000000 ) ) ;
#6818=ADVANCED_FACE ( 'NONE', ( #107605 ), #51826, .F. ) ;
#6819=VERTEX_POINT ( 'NONE', #83220 ) ;
#6820=EDGE_LOOP ( 'NONE', ( #50785, #100314, #95659, #64139, #78496 ) ) ;
#6822=EDGE_LOOP ( 'NONE', ( #17724, #122473, #53304, #36701 ) ) ;
#6823=LINE ( 'NONE', #128654, #98499 ) ;
#6824=CARTESIAN_POINT ( 'NONE',  ( -27.18398860626900060, 28.73617430169806042, 5.000000000000000000 ) ) ;
#6826=EDGE_CURVE ( 'NONE', #134910, #28590, #44875, .T. ) ;
#6827=DIRECTION ( 'NONE',  ( 0.7071067811865487940, 0.7071067811865463515, 0.000000000000000000 ) ) ;
#6829=ORIENTED_EDGE ( 'NONE', *, *, #68226, .T. ) ;
#6830=DIRECTION ( 'NONE',  ( -0.7071067811865486830, -0.7071067811865464625, 0.000000000000000000 ) ) ;
#6831=CARTESIAN_POINT ( 'NONE',  ( 22.49999999999984723, 8.319652575858409449, -8.582050562765775936 ) ) ;
#6832=CARTESIAN_POINT ( 'NONE',  ( -6.758600742197917732, 21.72500000000000142, 5.000000000000000000 ) ) ;
#6835=CARTESIAN_POINT ( 'NONE',  ( 31.49999999999977973, 1.030536316426536203, -5.498701923753874787 ) ) ;
#6836=EDGE_CURVE ( 'NONE', #134440, #41017, #40448, .T. ) ;
#6839=CARTESIAN_POINT ( 'NONE',  ( -10.17183060077640100, 9.759292476615614831, 4.000000000000000000 ) ) ;
#6840=VECTOR ( 'NONE', #129676, 1000.000000000000000 ) ;
#6841=ORIENTED_EDGE ( 'NONE', *, *, #27016, .F. ) ;
#6842=DIRECTION ( 'NONE',  ( -0.7071067811865487940, 0.7071067811865463515, -0.000000000000000000 ) ) ;
#6843=CARTESIAN_POINT ( 'NONE',  ( -11.99999999999991296, 17.58746187583907172, 4.000000000000000000 ) ) ;
#6844=AXIS2_PLACEMENT_3D ( 'NONE', #118490, #19190, #83029 ) ;
#6845=ORIENTED_EDGE ( 'NONE', *, *, #35653, .F. ) ;
#6846=ORIENTED_EDGE ( 'NONE', *, *, #141064, .T. ) ;
#6847=VERTEX_POINT ( 'NONE', #49182 ) ;
#6848=ADVANCED_FACE ( 'NONE', ( #71638 ), #139029, .T. ) ;
#6850=EDGE_CURVE ( 'NONE', #68379, #5793, #107094, .T. ) ;
#6851=VERTEX_POINT ( 'NONE', #28122 ) ;
#6853=ADVANCED_FACE ( 'NONE', ( #138312 ), #70934, .F. ) ;
#6854=VECTOR ( 'NONE', #22586, 1000.000000000000000 ) ;
#6858=DIRECTION ( 'NONE',  ( 1.000000000000000000, 0.000000000000000000, 0.000000000000000000 ) ) ;
#6859=ORIENTED_EDGE ( 'NONE', *, *, #134161, .T. ) ;
#6860=DIRECTION ( 'NONE',  ( 0.7071067811865486830, -0.7071067811865464625, -0.000000000000000000 ) ) ;
#6863=LINE ( 'NONE', #27948, #63752 ) ;
#6864=DIRECTION ( 'NONE',  ( 0.3543493200069162685, -0.000000000000000000, -0.9351131265310288487 ) ) ;
#6865=ORIENTED_EDGE ( 'NONE', *, *, #83552, .F. ) ;
#6866=EDGE_LOOP ( 'NONE', ( #47517, #22984, #11957, #58195 ) ) ;
#6867=PLANE ( 'NONE',  #134914 ) ;
#6868=ORIENTED_EDGE ( 'NONE', *, *, #27303, .T. ) ;
#6869=AXIS2_PLACEMENT_3D ( 'NONE', #79624, #89720, #111470 ) ;
#6870=CARTESIAN_POINT ( 'NONE',  ( -47.99451991528749062, 28.92564299267971251, 4.000000000000000000 ) ) ;
#6871=ORIENTED_EDGE ( 'NONE', *, *, #141831, .F. ) ;
#6872=ORIENTED_EDGE ( 'NONE', *, *, #31646, .F. ) ;
#6873=ORIENTED_EDGE ( 'NONE', *, *, #90651, .T. ) ;
#6874=ORIENTED_EDGE ( 'NONE', *, *, #63655, .F. ) ;
#6875=CARTESIAN_POINT ( 'NONE',  ( 31.82816939922331656, -17.24070752338409918, 4.000000000000000000 ) ) ;
#6876=AXIS2_PLACEMENT_3D ( 'NONE', #30913, #142528, #107723 ) ;
#6878=LINE ( 'NONE', #50443, #16737 ) ;
#6879=CARTESIAN_POINT ( 'NONE',  ( 11.99451991528749417, 28.92564299267946382, 4.000000000000000000 ) ) ;
#6880=CARTESIAN_POINT ( 'NONE',  ( -13.17183060077637968, -5.240707523384225297, 4.000000000000000000 ) ) ;
#6881=EDGE_LOOP ( 'NONE', ( #121944, #11650, #31354, #87855, #10531 ) ) ;
#6882=AXIS2_PLACEMENT_3D ( 'NONE', #126182, #115989, #71823 ) ;
#6883=CARTESIAN_POINT ( 'NONE',  ( -24.00548008471250938, 28.92564299267921513, 4.000000000000000000 ) ) ;
#6884=VERTEX_POINT ( 'NONE', #93375 ) ;
#6885=AXIS2_PLACEMENT_3D ( 'NONE', #112716, #135218, #134486 ) ;
#6886=CARTESIAN_POINT ( 'NONE',  ( -1.499999999999984013, -20.94781430457061333, 5.000000000000000000 ) ) ;
#6887=CARTESIAN_POINT ( 'NONE',  ( -28.49999999999980460, -5.568876922607759461, 4.000000000000000000 ) ) ;
#6888=DIRECTION ( 'NONE',  ( 0.6830127018922181881, 0.6830127018922202975, -0.2588190451025214056 ) ) ;
#6889=ORIENTED_EDGE ( 'NONE', *, *, #95363, .T. ) ;
#6890=CARTESIAN_POINT ( 'NONE',  ( -48.18398860626899705, 28.73617430169820608, 5.000000000000000000 ) ) ;
#6891=FACE_OUTER_BOUND ( 'NONE', #66405, .T. ) ;
#6892=ORIENTED_EDGE ( 'NONE', *, *, #108414, .T. ) ;
#6893=EDGE_LOOP ( 'NONE', ( #142897, #113266, #101994, #109541 ) ) ;
#6894=ORIENTED_EDGE ( 'NONE', *, *, #65304, .F. ) ;
#6895=FACE_OUTER_BOUND ( 'NONE', #19454, .T. ) ;
#6896=CARTESIAN_POINT ( 'NONE',  ( -13.84116387061258457, 6.089959206779446355, 4.000000000000000000 ) ) ;
#6897=AXIS2_PLACEMENT_3D ( 'NONE', #115506, #126414, #27105 ) ;
#6898=CARTESIAN_POINT ( 'NONE',  ( -12.18398860626900060, 28.73617430169795739, 5.000000000000000000 ) ) ;
#6901=LINE ( 'NONE', #50466, #71834 ) ;
#6902=CARTESIAN_POINT ( 'NONE',  ( 2.999999999999985345, -4.447814304570786526, 5.000000000000000000 ) ) ;
#6903=PLANE ( 'NONE',  #14058 ) ;
#6904=CARTESIAN_POINT ( 'NONE',  ( -1.499999999999977129, 13.08746187583910725, 4.000000000000000000 ) ) ;
#6905=DIRECTION ( 'NONE',  ( 0.3543493200069162685, -0.000000000000000000, -0.9351131265310288487 ) ) ;
#6906=ORIENTED_EDGE ( 'NONE', *, *, #96993, .F. ) ;
#6907=VECTOR ( 'NONE', #56874, 1000.000000000000000 ) ;
#6909=VERTEX_POINT ( 'NONE', #6304 ) ;
#6910=DIRECTION ( 'NONE',  ( -0.6830127018922180770, -0.6830127018922204085, -0.2588190451025213501 ) ) ;
#6913=EDGE_CURVE ( 'NONE', #69972, #30925, #94074, .T. ) ;
#6914=LINE ( 'NONE', #5509, #16241 ) ;
#6915=CARTESIAN_POINT ( 'NONE',  ( 27.29974487139158512, -27.71228299555225405, 4.000000000000000000 ) ) ;
#6916=ORIENTED_EDGE ( 'NONE', *, *, #110836, .F. ) ;
#6918=ORIENTED_EDGE ( 'NONE', *, *, #99925, .T. ) ;
#6919=CARTESIAN_POINT ( 'NONE',  ( 34.92499999999998295, -21.72500000000000142, 5.000000000000000000 ) ) ;
#6920=CARTESIAN_POINT ( 'NONE',  ( -11.95341186370447950, 14.25929247661557753, 18.84478104361330963 ) ) ;
#6921=VECTOR ( 'NONE', #67987, 1000.000000000000000 ) ;
#6922=AXIS2_PLACEMENT_3D ( 'NONE', #59554, #94286, #137090 ) ;
#6923=CARTESIAN_POINT ( 'NONE',  ( 32.99999999999976552, 5.966399257802198264, 5.000000000000000000 ) ) ;
#6925=CARTESIAN_POINT ( 'NONE',  ( 6.278254515685692816, 8.259292476615637923, 11.78515199841151784 ) ) ;
#6926=ORIENTED_EDGE ( 'NONE', *, *, #46304, .F. ) ;
#6927=EDGE_CURVE ( 'NONE', #2946, #9514, #139535, .T. ) ;
#6928=PLANE ( 'NONE',  #70113 ) ;
#6932=ORIENTED_EDGE ( 'NONE', *, *, #33885, .F. ) ;
#6933=ADVANCED_FACE ( 'NONE', ( #16503 ), #72387, .F. ) ;
#6934=LINE ( 'NONE', #115698, #28310 ) ;
#6935=ORIENTED_EDGE ( 'NONE', *, *, #62584, .F. ) ;
#6938=DIRECTION ( 'NONE',  ( -0.6830127018922180770, -0.6830127018922204085, -0.2588190451025213501 ) ) ;
#6941=FACE_OUTER_BOUND ( 'NONE', #140067, .T. ) ;
#6942=ORIENTED_EDGE ( 'NONE', *, *, #54087, .T. ) ;
#6943=ADVANCED_FACE ( 'NONE', ( #128848 ), #17913, .F. ) ;
#6944=AXIS2_PLACEMENT_3D ( 'NONE', #38508, #14609, #2264 ) ;
#6946=PLANE ( 'NONE',  #14125 ) ;
#6947=CARTESIAN_POINT ( 'NONE',  ( 13.49999999999991118, 7.466399257802187606, 5.000000000000000000 ) ) ;
#6949=VERTEX_POINT ( 'NONE', #105648 ) ;
#6951=CARTESIAN_POINT ( 'NONE',  ( -23.67183060077630330, -9.740707523384187994, 4.000000000000000000 ) ) ;
#6953=VECTOR ( 'NONE', #73667, 999.9999999999998863 ) ;
#6956=ORIENTED_EDGE ( 'NONE', *, *, #11537, .F. ) ;
#6957=ORIENTED_EDGE ( 'NONE', *, *, #116488, .F. ) ;
#6959=ORIENTED_EDGE ( 'NONE', *, *, #129952, .T. ) ;
#6960=EDGE_CURVE ( 'NONE', #23280, #76403, #60793, .T. ) ;
#6961=CARTESIAN_POINT ( 'NONE',  ( 24.61500991739762512, 5.335133370053847912, 4.556819239218476980 ) ) ;
#6962=DIRECTION ( 'NONE',  ( 0.7071067811865486830, -0.7071067811865464625, -0.000000000000000000 ) ) ;
#6963=ORIENTED_EDGE ( 'NONE', *, *, #108799, .T. ) ;
#6964=LINE ( 'NONE', #38231, #23597 ) ;
#6965=CARTESIAN_POINT ( 'NONE',  ( -34.92500000000001137, 4.701930566820959001, 4.500000000000000888 ) ) ;
#6968=VECTOR ( 'NONE', #11977, 1000.000000000000000 ) ;
#6970=VECTOR ( 'NONE', #133661, 1000.000000000000000 ) ;
#6971=LINE ( 'NONE', #52660, #51317 ) ;
#6972=AXIS2_PLACEMENT_3D ( 'NONE', #72983, #127310, #72280 ) ;
#6974=CARTESIAN_POINT ( 'NONE',  ( -15.69326993309589824, -3.740707523384244837, 12.88036043432871303 ) ) ;
#6976=EDGE_CURVE ( 'NONE', #34897, #123482, #90752, .T. ) ;
#6977=VERTEX_POINT ( 'NONE', #134982 ) ;
#6978=VERTEX_POINT ( 'NONE', #33526 ) ;
#6979=EDGE_CURVE ( 'NONE', #131599, #107344, #24753, .T. ) ;
#6980=AXIS2_PLACEMENT_3D ( 'NONE', #51173, #74358, #118547 ) ;
#6983=CARTESIAN_POINT ( 'NONE',  ( 8.816011393731004731, 28.73617430169781173, 5.000000000000000000 ) ) ;
#6984=LINE ( 'NONE', #51268, #115916 ) ;
#6985=LINE ( 'NONE', #19166, #10845 ) ;
#6986=CARTESIAN_POINT ( 'NONE',  ( -29.29289321881325137, 11.25929247661560773, 5.000000000000000000 ) ) ;
#6987=CARTESIAN_POINT ( 'NONE',  ( -34.92500000000001137, 8.454535441273645091, -0.2181437882982119325 ) ) ;
#6988=CARTESIAN_POINT ( 'NONE',  ( -18.00548008471250583, 28.92564299267925776, 4.000000000000000000 ) ) ;
#6990=ORIENTED_EDGE ( 'NONE', *, *, #62319, .F. ) ;
#6991=VECTOR ( 'NONE', #135949, 1000.000000000000000 ) ;
#6992=EDGE_LOOP ( 'NONE', ( #77970, #136678, #113297, #52716 ) ) ;
#6993=VERTEX_POINT ( 'NONE', #25452 ) ;
#6995=EDGE_LOOP ( 'NONE', ( #18463, #60264, #47235, #77607 ) ) ;
#6997=ADVANCED_FACE ( 'NONE', ( #26895 ), #138522, .F. ) ;
#6999=EDGE_LOOP ( 'NONE', ( #136960, #90877, #109230, #54714 ) ) ;
#7000=DIRECTION ( 'NONE',  ( -0.7071067811865487940, 0.7071067811865463515, -0.000000000000000000 ) ) ;
#7001=LINE ( 'NONE', #138286, #123633 ) ;
#7002=CARTESIAN_POINT ( 'NONE',  ( -11.99999999999991651, -21.84840872380825516, 2.849755605029579808 ) ) ;
#7003=CARTESIAN_POINT ( 'NONE',  ( -30.48921356237309510, -27.52281430457076894, 5.000000000000000000 ) ) ;
#7005=FACE_OUTER_BOUND ( 'NONE', #56984, .T. ) ;
#7006=VERTEX_POINT ( 'NONE', #50797 ) ;
#7007=DIRECTION ( 'NONE',  ( -0.3543493200069163240, 4.681814790819596721E-17, -0.9351131265310288487 ) ) ;
#7008=DIRECTION ( 'NONE',  ( -0.7071067811865487940, 0.7071067811865463515, 0.000000000000000000 ) ) ;
#7009=ORIENTED_EDGE ( 'NONE', *, *, #4630, .T. ) ;
#7010=FACE_OUTER_BOUND ( 'NONE', #56009, .T. ) ;
#7011=ORIENTED_EDGE ( 'NONE', *, *, #14340, .F. ) ;
#7012=CARTESIAN_POINT ( 'NONE',  ( -9.516654386410381861, 22.22500000000000142, 4.500000000000000888 ) ) ;
#7013=ORIENTED_EDGE ( 'NONE', *, *, #14904, .T. ) ;
#7016=VECTOR ( 'NONE', #87919, 1000.000000000000000 ) ;
#7017=ORIENTED_EDGE ( 'NONE', *, *, #132423, .T. ) ;
#7018=VECTOR ( 'NONE', #139968, 1000.000000000000227 ) ;
#7019=EDGE_CURVE ( 'NONE', #88713, #22841, #17438, .T. ) ;
#7020=DIRECTION ( 'NONE',  ( -0.7071067811865487940, 0.7071067811865463515, -0.000000000000000000 ) ) ;
#7021=ADVANCED_FACE ( 'NONE', ( #137092 ), #60268, .F. ) ;
#7022=DIRECTION ( 'NONE',  ( 0.7071067811865486830, -0.7071067811865464625, -0.000000000000000000 ) ) ;
#7024=DIRECTION ( 'NONE',  ( -0.7071067811865486830, -0.7071067811865464625, 0.000000000000000000 ) ) ;
#7025=DIRECTION ( 'NONE',  ( 0.7071067811865487940, -0.7071067811865463515, 0.000000000000000000 ) ) ;
#7026=CARTESIAN_POINT ( 'NONE',  ( -33.18398860626899705, 28.73617430169810305, 5.000000000000000000 ) ) ;
#7027=CARTESIAN_POINT ( 'NONE',  ( -14.97558742549547617, -1.187250289053312979, 4.247958624336151345 ) ) ;
#7028=VECTOR ( 'NONE', #87830, 1000.000000000000000 ) ;
#7029=ADVANCED_FACE ( 'NONE', ( #129773 ), #42796, .F. ) ;
#7033=DIRECTION ( 'NONE',  ( -0.7071067811865486830, 0.7071067811865463515, 0.000000000000000000 ) ) ;
#7034=VECTOR ( 'NONE', #90270, 1000.000000000000000 ) ;
#7036=CARTESIAN_POINT ( 'NONE',  ( 16.82816939922341604, 15.75929247661555088, 4.000000000000000000 ) ) ;
#7037=CARTESIAN_POINT ( 'NONE',  ( -9.707106781186469746, -9.740707523384184441, 5.000000000000000000 ) ) ;
#7038=ORIENTED_EDGE ( 'NONE', *, *, #30062, .F. ) ;
#7039=EDGE_LOOP ( 'NONE', ( #33735, #30643, #65578, #33320 ) ) ;
#7040=CARTESIAN_POINT ( 'NONE',  ( 62.99451991528749772, 28.92564299267982264, 4.000000000000000000 ) ) ;
#7041=AXIS2_PLACEMENT_3D ( 'NONE', #121586, #143345, #53497 ) ;
#7042=ORIENTED_EDGE ( 'NONE', *, *, #102614, .T. ) ;
#7043=VECTOR ( 'NONE', #72254, 1000.000000000000000 ) ;
#7045=VECTOR ( 'NONE', #39559, 999.9999999999998863 ) ;
#7046=DIRECTION ( 'NONE',  ( 0.3543493200069163240, 0.000000000000000000, 0.9351131265310288487 ) ) ;
#7047=CARTESIAN_POINT ( 'NONE',  ( -13.82816939922344091, -17.24070752338409918, 4.000000000000000000 ) ) ;
#7048=CARTESIAN_POINT ( 'NONE',  ( -42.48921356237308800, -27.52281430457085065, 5.000000000000000000 ) ) ;
#7049=DIRECTION ( 'NONE',  ( -0.3543493200069162685, -0.000000000000000000, -0.9351131265310288487 ) ) ;
#7050=ORIENTED_EDGE ( 'NONE', *, *, #128520, .F. ) ;
#7053=VERTEX_POINT ( 'NONE', #56554 ) ;
#7055=CARTESIAN_POINT ( 'NONE',  ( -11.20666063542143753, 21.75929247661549937, 4.998822639870708073 ) ) ;
#7056=CARTESIAN_POINT ( 'NONE',  ( 63.18398860626900415, 28.73617430169831621, 5.000000000000000000 ) ) ;
#7057=CARTESIAN_POINT ( 'NONE',  ( 10.49999999999993072, 15.05218569542901896, 5.000000000000000000 ) ) ;
#7058=EDGE_LOOP ( 'NONE', ( #28381, #142275, #4915, #27729 ) ) ;
#7059=VERTEX_POINT ( 'NONE', #88431 ) ;
#7060=EDGE_CURVE ( 'NONE', #64733, #14309, #31892, .T. ) ;
#7064=LINE ( 'NONE', #41160, #136742 ) ;
#7065=CARTESIAN_POINT ( 'NONE',  ( 13.49999999999990763, 8.900465351122162971, -2.516491619111544953 ) ) ;
#7067=FACE_OUTER_BOUND ( 'NONE', #97351, .T. ) ;
#7068=DIRECTION ( 'NONE',  ( -0.7071067811865486830, -0.7071067811865464625, 0.000000000000000000 ) ) ;
#7069=CARTESIAN_POINT ( 'NONE',  ( 5.700255128608413102, -27.71228299555201957, 4.000000000000000000 ) ) ;
#7070=VECTOR ( 'NONE', #110395, 1000.000000000000000 ) ;
#7071=VECTOR ( 'NONE', #80141, 1000.000000000000227 ) ;
#7074=LINE ( 'NONE', #7813, #141478 ) ;
#7075=VECTOR ( 'NONE', #3045, 1000.000000000000114 ) ;
#7076=VERTEX_POINT ( 'NONE', #120281 ) ;
#7077=DIRECTION ( 'NONE',  ( -0.000000000000000000, 0.3543493200069153248, 0.9351131265310292928 ) ) ;
#7078=CARTESIAN_POINT ( 'NONE',  ( 54.18398860626899705, 28.73617430169825226, 5.000000000000000000 ) ) ;
#7079=ORIENTED_EDGE ( 'NONE', *, *, #113747, .F. ) ;
#7081=CARTESIAN_POINT ( 'NONE',  ( -0.2997448713915885632, -27.71228299555206220, 4.000000000000000000 ) ) ;
#7082=CARTESIAN_POINT ( 'NONE',  ( 4.930039745135884388, -0.7407075233842770334, 13.87443053587610109 ) ) ;
#7086=LINE ( 'NONE', #38340, #116349 ) ;
#7088=ORIENTED_EDGE ( 'NONE', *, *, #100826, .F. ) ;
#7089=DIRECTION ( 'NONE',  ( -0.7071067811865486830, -0.7071067811865464625, 0.000000000000000000 ) ) ;
#7091=EDGE_LOOP ( 'NONE', ( #110812, #131178, #76099, #72331 ) ) ;
#7092=EDGE_CURVE ( 'NONE', #74581, #53159, #86811, .T. ) ;
#7093=EDGE_CURVE ( 'NONE', #138830, #18068, #10746, .T. ) ;
#7094=FACE_OUTER_BOUND ( 'NONE', #46231, .T. ) ;
#7096=LINE ( 'NONE', #4213, #120270 ) ;
#7098=CARTESIAN_POINT ( 'NONE',  ( 30.29974487139158867, -27.71228299555227537, 4.000000000000000000 ) ) ;
#7099=EDGE_CURVE ( 'NONE', #53161, #80396, #97792, .T. ) ;
#7101=DIRECTION ( 'NONE',  ( 0.7071067811865487940, 0.7071067811865463515, 0.000000000000000000 ) ) ;
#7103=AXIS2_PLACEMENT_3D ( 'NONE', #130941, #125596, #26271 ) ;
#7105=DIRECTION ( 'NONE',  ( -0.7071067811865486830, -0.7071067811865464625, 0.000000000000000000 ) ) ;
#7106=CARTESIAN_POINT ( 'NONE',  ( 7.171830600776425868, 3.759292476615681888, 4.000000000000000000 ) ) ;
#7108=ORIENTED_EDGE ( 'NONE', *, *, #142417, .T. ) ;
#7110=EDGE_CURVE ( 'NONE', #89257, #37221, #120220, .T. ) ;
#7111=CARTESIAN_POINT ( 'NONE',  ( 0.000000000000000000, 0.000000000000000000, 5.000000000000000000 ) ) ;
#7112=VERTEX_POINT ( 'NONE', #108633 ) ;
#7113=DIRECTION ( 'NONE',  ( -0.7071067811865487940, 0.7071067811865463515, -0.000000000000000000 ) ) ;
#7116=LINE ( 'NONE', #126103, #6048 ) ;
#7117=ORIENTED_EDGE ( 'NONE', *, *, #138129, .F. ) ;
#7118=EDGE_CURVE ( 'NONE', #136547, #23940, #74638, .T. ) ;
#7119=CARTESIAN_POINT ( 'NONE',  ( 31.17183060077625356, -5.240707523384228850, 4.000000000000000000 ) ) ;
#7120=CARTESIAN_POINT ( 'NONE',  ( 14.70025512860841133, -27.71228299555195917, 4.000000000000000000 ) ) ;
#7121=CARTESIAN_POINT ( 'NONE',  ( 39.29974487139159578, -27.71228299555233576, 4.000000000000000000 ) ) ;
#7122=LINE ( 'NONE', #73857, #90994 ) ;
#7123=DIRECTION ( 'NONE',  ( 0.7071067811865486830, -0.7071067811865464625, -0.000000000000000000 ) ) ;
#7124=ADVANCED_FACE ( 'NONE', ( #44144 ), #65197, .F. ) ;
#7125=FACE_OUTER_BOUND ( 'NONE', #67752, .T. ) ;
#7126=AXIS2_PLACEMENT_3D ( 'NONE', #121087, #57304, #111657 ) ;
#7127=CARTESIAN_POINT ( 'NONE',  ( 0.000000000000000000, 0.000000000000000000, 5.000000000000000000 ) ) ;
#7128=FACE_OUTER_BOUND ( 'NONE', #43965, .T. ) ;
#7129=DIRECTION ( 'NONE',  ( -0.7071067811865487940, 0.7071067811865463515, 0.000000000000000000 ) ) ;
#7132=EDGE_LOOP ( 'NONE', ( #126882, #93561, #23473, #96035 ) ) ;
#7134=ORIENTED_EDGE ( 'NONE', *, *, #91906, .F. ) ;
#7135=EDGE_CURVE ( 'NONE', #130377, #58822, #131142, .T. ) ;
#7136=CARTESIAN_POINT ( 'NONE',  ( 26.12514619309218133, -14.24070752338413470, 9.401115078912598122 ) ) ;
#7137=CARTESIAN_POINT ( 'NONE',  ( -23.81601139373100295, 28.73617430169770870, 5.000000000000000000 ) ) ;
#7138=ORIENTED_EDGE ( 'NONE', *, *, #26163, .F. ) ;
#7140=CARTESIAN_POINT ( 'NONE',  ( 38.99451991528749062, 28.92564299267965211, 4.000000000000000000 ) ) ;
#7141=CARTESIAN_POINT ( 'NONE',  ( 60.48921356237309510, -27.52281430457097500, 5.000000000000000000 ) ) ;
#7143=EDGE_CURVE ( 'NONE', #128780, #91002, #132607, .T. ) ;
#7144=AXIS2_PLACEMENT_3D ( 'NONE', #110066, #122367, #61793 ) ;
#7147=EDGE_CURVE ( 'NONE', #81467, #102769, #9307, .T. ) ;
#7148=LINE ( 'NONE', #63036, #18788 ) ;
#7149=ORIENTED_EDGE ( 'NONE', *, *, #29776, .F. ) ;
#7150=DIRECTION ( 'NONE',  ( 1.000000000000000000, 0.000000000000000000, 0.000000000000000000 ) ) ;
#7151=VECTOR ( 'NONE', #124616, 1000.000000000000000 ) ;
#7152=VECTOR ( 'NONE', #52600, 1000.000000000000000 ) ;
#7154=VECTOR ( 'NONE', #67798, 1000.000000000000000 ) ;
#7155=AXIS2_PLACEMENT_3D ( 'NONE', #37702, #79084, #113083 ) ;
#7156=CARTESIAN_POINT ( 'NONE',  ( 0.2997448713915885632, -27.71228299555206220, 4.000000000000000000 ) ) ;
#7157=EDGE_CURVE ( 'NONE', #103619, #82336, #66609, .T. ) ;
#7158=VECTOR ( 'NONE', #55983, 1000.000000000000000 ) ;
#7159=VERTEX_POINT ( 'NONE', #98507 ) ;
#7160=ORIENTED_EDGE ( 'NONE', *, *, #59069, .T. ) ;
#7161=ORIENTED_EDGE ( 'NONE', *, *, #113885, .T. ) ;
#7162=DIRECTION ( 'NONE',  ( 0.3543493200069162685, -0.000000000000000000, -0.9351131265310288487 ) ) ;
#7163=DIRECTION ( 'NONE',  ( -0.7071067811865486830, -0.7071067811865464625, -0.000000000000000000 ) ) ;
#7165=AXIS2_PLACEMENT_3D ( 'NONE', #30168, #74415, #20712 ) ;
#7166=LINE ( 'NONE', #50017, #87316 ) ;
#7167=ORIENTED_EDGE ( 'NONE', *, *, #103846, .F. ) ;
#7168=VERTEX_POINT ( 'NONE', #63762 ) ;
#7170=ADVANCED_FACE ( 'NONE', ( #121668 ), #142731, .T. ) ;
#7171=LINE ( 'NONE', #115945, #68719 ) ;
#7172=ORIENTED_EDGE ( 'NONE', *, *, #121256, .T. ) ;
#7173=ORIENTED_EDGE ( 'NONE', *, *, #117622, .F. ) ;
#7175=EDGE_CURVE ( 'NONE', #109845, #94724, #99943, .T. ) ;
#7176=VECTOR ( 'NONE', #133618, 1000.000000000000000 ) ;
#7177=CARTESIAN_POINT ( 'NONE',  ( 6.328169399223492420, -0.7407075233842735917, 4.000000000000000000 ) ) ;
#7179=ORIENTED_EDGE ( 'NONE', *, *, #89538, .T. ) ;
#7180=FACE_OUTER_BOUND ( 'NONE', #107301, .T. ) ;
#7181=AXIS2_PLACEMENT_3D ( 'NONE', #85491, #53617, #88393 ) ;
#7183=DIRECTION ( 'NONE',  ( -0.000000000000000000, -0.3543493200069152693, 0.9351131265310292928 ) ) ;
#7184=VECTOR ( 'NONE', #12473, 999.9999999999998863 ) ;
#7186=ORIENTED_EDGE ( 'NONE', *, *, #17084, .T. ) ;
#7187=PLANE ( 'NONE',  #85719 ) ;
#7188=LINE ( 'NONE', #118838, #50045 ) ;
#7189=VERTEX_POINT ( 'NONE', #110084 ) ;
#7190=LINE ( 'NONE', #84792, #4017 ) ;
#7191=PLANE ( 'NONE',  #142982 ) ;
#7192=VECTOR ( 'NONE', #137849, 1000.000000000000000 ) ;
#7193=DIRECTION ( 'NONE',  ( -0.7071067811865487940, 0.7071067811865463515, -0.000000000000000000 ) ) ;
#7194=EDGE_CURVE ( 'NONE', #116279, #141681, #52837, .T. ) ;
#7195=ORIENTED_EDGE ( 'NONE', *, *, #92385, .T. ) ;
#7196=LINE ( 'NONE', #107250, #73664 ) ;
#7197=EDGE_LOOP ( 'NONE', ( #22983, #18619, #5587, #136048, #141619 ) ) ;
#7198=EDGE_LOOP ( 'NONE', ( #80305, #4114, #115885, #110226 ) ) ;
#7199=EDGE_LOOP ( 'NONE', ( #78162, #11306, #41333, #68225 ) ) ;
#7200=EDGE_CURVE ( 'NONE', #12371, #81437, #21669, .T. ) ;
#7201=DIRECTION ( 'NONE',  ( 0.7071067811865487940, 0.7071067811865463515, 0.000000000000000000 ) ) ;
#7202=VECTOR ( 'NONE', #12015, 1000.000000000000000 ) ;
#7203=DIRECTION ( 'NONE',  ( -0.7071067811865486830, -0.7071067811865464625, -0.000000000000000000 ) ) ;
#7204=PLANE ( 'NONE',  #10119 ) ;
#7205=CARTESIAN_POINT ( 'NONE',  ( 45.48921356237309510, -27.52281430457087197, 5.000000000000000000 ) ) ;
#7207=CARTESIAN_POINT ( 'NONE',  ( 17.99999999999987210, -6.108550654416944781, -3.114665004254924430 ) ) ;
#7208=AXIS2_PLACEMENT_3D ( 'NONE', #52626, #121455, #109873 ) ;
#7209=CARTESIAN_POINT ( 'NONE',  ( 30.48921356237309510, -27.52281430457076894, 5.000000000000000000 ) ) ;
#7211=LINE ( 'NONE', #62364, #35293 ) ;
#7212=EDGE_CURVE ( 'NONE', #128869, #90647, #76793, .T. ) ;
#7213=LINE ( 'NONE', #84812, #8835 ) ;
#7214=LINE ( 'NONE', #126183, #126919 ) ;
#7215=DIRECTION ( 'NONE',  ( 1.000000000000000000, -0.000000000000000000, 0.000000000000000000 ) ) ;
#7217=VERTEX_POINT ( 'NONE', #42729 ) ;
#7219=ORIENTED_EDGE ( 'NONE', *, *, #133389, .F. ) ;
#7220=AXIS2_PLACEMENT_3D ( 'NONE', #22072, #88068, #120664 ) ;
#7221=ORIENTED_EDGE ( 'NONE', *, *, #58596, .F. ) ;
#7225=VERTEX_POINT ( 'NONE', #65918 ) ;
#7226=FACE_OUTER_BOUND ( 'NONE', #96435, .T. ) ;
#7228=DIRECTION ( 'NONE',  ( 0.7071067811865487940, 0.7071067811865463515, 0.000000000000000000 ) ) ;
#7230=PLANE ( 'NONE',  #27787 ) ;
#7231=ORIENTED_EDGE ( 'NONE', *, *, #91310, .T. ) ;
#7232=DIRECTION ( 'NONE',  ( 0.7071067811865487940, -0.7071067811865463515, 0.000000000000000000 ) ) ;
#7234=EDGE_LOOP ( 'NONE', ( #132066, #31674, #84211, #26323 ) ) ;
#7235=LINE ( 'NONE', #98554, #72217 ) ;
#7238=VERTEX_POINT ( 'NONE', #42004 ) ;
#7240=LINE ( 'NONE', #139960, #76024 ) ;
#7241=DIRECTION ( 'NONE',  ( -0.7071067811865486830, -0.7071067811865464625, -0.000000000000000000 ) ) ;
#7242=LINE ( 'NONE', #95709, #129914 ) ;
#7246=ORIENTED_EDGE ( 'NONE', *, *, #18565, .T. ) ;
#7247=CARTESIAN_POINT ( 'NONE',  ( -9.183988606268997046, 28.73617430169793607, 5.000000000000000000 ) ) ;
#7248=CARTESIAN_POINT ( 'NONE',  ( 60.29974487139158867, -27.71228299555248142, 4.000000000000000000 ) ) ;
#7249=AXIS2_PLACEMENT_3D ( 'NONE', #93403, #28151, #26012 ) ;
#7250=CARTESIAN_POINT ( 'NONE',  ( -24.18398860626899705, 28.73617430169804265, 5.000000000000000000 ) ) ;
#7251=CARTESIAN_POINT ( 'NONE',  ( -9.098435806082317612, 11.25929247661560240, 10.79108189686405161 ) ) ;
#7252=ORIENTED_EDGE ( 'NONE', *, *, #48260, .F. ) ;
#7253=AXIS2_PLACEMENT_3D ( 'NONE', #93018, #69881, #57559 ) ;
#7254=CARTESIAN_POINT ( 'NONE',  ( -35.99451991528749772, 28.92564299267963079, 4.000000000000000000 ) ) ;
#7255=VECTOR ( 'NONE', #118645, 999.9999999999998863 ) ;
#7257=LINE ( 'NONE', #130522, #109113 ) ;
#7258=LINE ( 'NONE', #142116, #118271 ) ;
#7259=EDGE_CURVE ( 'NONE', #8140, #91460, #80358, .T. ) ;
#7260=ORIENTED_EDGE ( 'NONE', *, *, #67317, .F. ) ;
#7261=FACE_OUTER_BOUND ( 'NONE', #50879, .T. ) ;
#7264=VECTOR ( 'NONE', #52657, 1000.000000000000000 ) ;
#7265=LINE ( 'NONE', #61705, #738 ) ;
#7267=VERTEX_POINT ( 'NONE', #122384 ) ;
#7269=EDGE_LOOP ( 'NONE', ( #2372, #106241, #31717, #97864 ) ) ;
#7270=EDGE_CURVE ( 'NONE', #64780, #54692, #24515, .T. ) ;
#7271=ADVANCED_FACE ( 'NONE', ( #89763 ), #57897, .F. ) ;
#7272=CARTESIAN_POINT ( 'NONE',  ( -9.693269933095928437, -3.740707523384244837, 12.88036043432869882 ) ) ;
#7273=AXIS2_PLACEMENT_3D ( 'NONE', #47529, #72129, #114153 ) ;
#7274=DIRECTION ( 'NONE',  ( 0.7071067811865486830, -0.7071067811865464625, -0.000000000000000000 ) ) ;
#7275=ORIENTED_EDGE ( 'NONE', *, *, #122326, .T. ) ;
#7276=DIRECTION ( 'NONE',  ( 0.7071067811865486830, -0.7071067811865464625, -0.000000000000000000 ) ) ;
#7278=ADVANCED_FACE ( 'NONE', ( #23812 ), #100666, .F. ) ;
#7279=CARTESIAN_POINT ( 'NONE',  ( 14.20666063542142687, 21.75929247661549937, 4.998822639870700080 ) ) ;
#7280=LINE ( 'NONE', #74003, #36803 ) ;
#7281=EDGE_CURVE ( 'NONE', #118169, #126680, #103481, .T. ) ;
#7282=VECTOR ( 'NONE', #2382, 1000.000000000000000 ) ;
#7284=CARTESIAN_POINT ( 'NONE',  ( -78.48921356237309510, -27.52281430457109934, 5.000000000000000000 ) ) ;
#7285=EDGE_CURVE ( 'NONE', #23427, #56845, #34696, .T. ) ;
#7286=LINE ( 'NONE', #129801, #11997 ) ;
#7287=DIRECTION ( 'NONE',  ( 0.7071067811865487940, 0.7071067811865463515, 0.000000000000000000 ) ) ;
#7288=DIRECTION ( 'NONE',  ( 0.7071067811865487940, -0.7071067811865463515, 0.000000000000000000 ) ) ;
#7289=CARTESIAN_POINT ( 'NONE',  ( 14.99999999999990941, -19.44781430457063465, 5.000000000000000000 ) ) ;
#7290=CARTESIAN_POINT ( 'NONE',  ( 21.11237052021067129, 8.776708805967446736, 4.202873650309270737 ) ) ;
#7291=EDGE_CURVE ( 'NONE', #130333, #121313, #45594, .T. ) ;
#7292=DIRECTION ( 'NONE',  ( 0.7071067811865486830, -0.7071067811865464625, -0.000000000000000000 ) ) ;
#7293=ORIENTED_EDGE ( 'NONE', *, *, #61025, .T. ) ;
#7294=VECTOR ( 'NONE', #108639, 1000.000000000000227 ) ;
#7295=EDGE_LOOP ( 'NONE', ( #51413, #51817, #49134 ) ) ;
#7296=ORIENTED_EDGE ( 'NONE', *, *, #80533, .F. ) ;
#7299=VECTOR ( 'NONE', #94017, 1000.000000000000000 ) ;
#7300=ORIENTED_EDGE ( 'NONE', *, *, #3295, .F. ) ;
#7301=EDGE_LOOP ( 'NONE', ( #115354, #8356, #21460, #17902 ) ) ;
#7303=ORIENTED_EDGE ( 'NONE', *, *, #14860, .T. ) ;
#7304=PLANE ( 'NONE',  #140451 ) ;
#7306=VECTOR ( 'NONE', #105718, 999.9999999999998863 ) ;
#7307=ORIENTED_EDGE ( 'NONE', *, *, #5932, .T. ) ;
#7308=DIRECTION ( 'NONE',  ( -8.817971600062199903E-18, 0.3543493200069153248, 0.9351131265310292928 ) ) ;
#7309=EDGE_CURVE ( 'NONE', #4615, #57316, #35439, .T. ) ;
#7310=FACE_OUTER_BOUND ( 'NONE', #108390, .T. ) ;
#7311=CARTESIAN_POINT ( 'NONE',  ( 25.49999999999981881, -20.56887692260760758, 4.000000000000000000 ) ) ;
#7314=ORIENTED_EDGE ( 'NONE', *, *, #6359, .T. ) ;
#7315=LINE ( 'NONE', #84900, #64999 ) ;
#7316=DIRECTION ( 'NONE',  ( 0.3543493200069162685, -0.000000000000000000, -0.9351131265310288487 ) ) ;
#7317=DIRECTION ( 'NONE',  ( -0.000000000000000000, 1.000000000000000000, -0.000000000000000000 ) ) ;
#7318=DIRECTION ( 'NONE',  ( -0.7071067811865487940, 0.7071067811865463515, -0.000000000000000000 ) ) ;
#7320=AXIS2_PLACEMENT_3D ( 'NONE', #53219, #97432, #9715 ) ;
#7321=DIRECTION ( 'NONE',  ( 0.7071067811865487940, 0.7071067811865463515, -0.000000000000000000 ) ) ;
#7324=CARTESIAN_POINT ( 'NONE',  ( 13.49999999999991473, -4.796895815301002841, -3.611700055028651768 ) ) ;
#7329=CARTESIAN_POINT ( 'NONE',  ( 0.4892135623730947680, -27.52281430457055578, 5.000000000000000000 ) ) ;
#7330=VECTOR ( 'NONE', #42157, 1000.000000000000000 ) ;
#7331=LINE ( 'NONE', #84241, #128849 ) ;
#7332=VECTOR ( 'NONE', #113204, 1000.000000000000000 ) ;
#7333=DIRECTION ( 'NONE',  ( -0.000000000000000000, -0.000000000000000000, 1.000000000000000000 ) ) ;
#7334=CARTESIAN_POINT ( 'NONE',  ( -36.48921356237310221, -27.52281430457080802, 5.000000000000000000 ) ) ;
#7337=ADVANCED_FACE ( 'NONE', ( #57185 ), #23056, .T. ) ;
#7339=VERTEX_POINT ( 'NONE', #101360 ) ;
#7340=VECTOR ( 'NONE', #141143, 1000.000000000000000 ) ;
#7341=EDGE_CURVE ( 'NONE', #44042, #109431, #90498, .T. ) ;
#7342=LINE ( 'NONE', #73360, #105817 ) ;
#7344=VECTOR ( 'NONE', #34773, 999.9999999999998863 ) ;
#7345=PLANE ( 'NONE',  #73995 ) ;
#7346=CARTESIAN_POINT ( 'NONE',  ( -36.48921356237310221, -27.52281430457080802, 5.000000000000000000 ) ) ;
#7347=DIRECTION ( 'NONE',  ( -0.3543493200069162685, -0.000000000000000000, -0.9351131265310288487 ) ) ;
#7348=ADVANCED_FACE ( 'NONE', ( #58642 ), #3451, .F. ) ;
#7349=CARTESIAN_POINT ( 'NONE',  ( 16.49999999999989342, 19.46639925780206326, 5.000000000000000000 ) ) ;
#7350=ORIENTED_EDGE ( 'NONE', *, *, #141290, .T. ) ;
#7352=ORIENTED_EDGE ( 'NONE', *, *, #108613, .T. ) ;
#7353=DIRECTION ( 'NONE',  ( 1.000000000000000000, 0.000000000000000000, 0.000000000000000000 ) ) ;
#7354=LINE ( 'NONE', #52301, #83193 ) ;
#7355=DIRECTION ( 'NONE',  ( -0.7071067811865486830, -0.7071067811865464625, 0.000000000000000000 ) ) ;
#7358=( BOUNDED_CURVE ( )  B_SPLINE_CURVE ( 3, ( #91355, #9638, #53916, #68200 ),
 .UNSPECIFIED., .F., .T. ) 
 B_SPLINE_CURVE_WITH_KNOTS ( ( 4, 4 ),
 ( 1.862445515227526771, 1.909667095125055392 ),
 .UNSPECIFIED. ) 
 CURVE ( )  GEOMETRIC_REPRESENTATION_ITEM ( )  RATIONAL_B_SPLINE_CURVE ( ( 1.000000000000000000, 0.9998141854983972898, 0.9998141854983972898, 1.000000000000000000 ) ) 
 REPRESENTATION_ITEM ( '' )  );
#7360=ORIENTED_EDGE ( 'NONE', *, *, #46994, .T. ) ;
#7361=CARTESIAN_POINT ( 'NONE',  ( -54.48921356237310221, -27.52281430457093236, 5.000000000000000000 ) ) ;
#7362=ADVANCED_FACE ( 'NONE', ( #36814 ), #81061, .F. ) ;
#7363=CARTESIAN_POINT ( 'NONE',  ( 57.48921356237308800, -27.52281430457095368, 5.000000000000000000 ) ) ;
#7364=ORIENTED_EDGE ( 'NONE', *, *, #110406, .F. ) ;
#7365=VERTEX_POINT ( 'NONE', #15050 ) ;
#7366=VERTEX_POINT ( 'NONE', #59329 ) ;
#7368=LINE ( 'NONE', #137924, #34971 ) ;
#7369=ADVANCED_FACE ( 'NONE', ( #48410 ), #92609, .F. ) ;
#7370=EDGE_LOOP ( 'NONE', ( #6290, #122072, #101683, #27540 ) ) ;
#7372=VECTOR ( 'NONE', #93983, 1000.000000000000000 ) ;
#7373=FACE_OUTER_BOUND ( 'NONE', #5237, .T. ) ;
#7374=VECTOR ( 'NONE', #74391, 1000.000000000000000 ) ;
#7375=VECTOR ( 'NONE', #3938, 999.9999999999998863 ) ;
#7377=EDGE_CURVE ( 'NONE', #141023, #100787, #51284, .T. ) ;
#7378=FACE_BOUND ( 'NONE', #60718, .T. ) ;
#7379=CARTESIAN_POINT ( 'NONE',  ( -57.48921356237308800, -27.52281430457095368, 5.000000000000000000 ) ) ;
#7381=EDGE_CURVE ( 'NONE', #55035, #135278, #81791, .T. ) ;
#7382=ORIENTED_EDGE ( 'NONE', *, *, #7986, .F. ) ;
#7384=ORIENTED_EDGE ( 'NONE', *, *, #33496, .F. ) ;
#7385=ORIENTED_EDGE ( 'NONE', *, *, #116968, .F. ) ;
#7386=DIRECTION ( 'NONE',  ( -0.000000000000000000, 0.3543493200069153248, 0.9351131265310292928 ) ) ;
#7387=EDGE_LOOP ( 'NONE', ( #51138, #139168, #4723, #28131 ) ) ;
#7390=VERTEX_POINT ( 'NONE', #104185 ) ;
#7391=LINE ( 'NONE', #116178, #4676 ) ;
#7393=ORIENTED_EDGE ( 'NONE', *, *, #11779, .F. ) ;
#7394=FACE_OUTER_BOUND ( 'NONE', #94620, .T. ) ;
#7395=EDGE_CURVE ( 'NONE', #26993, #67807, #60019, .T. ) ;
#7396=VECTOR ( 'NONE', #133839, 1000.000000000000000 ) ;
#7397=VECTOR ( 'NONE', #69274, 1000.000000000000227 ) ;
#7399=DIRECTION ( 'NONE',  ( -0.7071067811865486830, 0.7071067811865464625, 0.000000000000000000 ) ) ;
#7400=DIRECTION ( 'NONE',  ( -0.7071067811865486830, -0.7071067811865464625, 0.000000000000000000 ) ) ;
#7401=CARTESIAN_POINT ( 'NONE',  ( -8.953411863704499041, 14.25929247661557753, 18.84478104361330253 ) ) ;
#7402=AXIS2_PLACEMENT_3D ( 'NONE', #71651, #94087, #138325 ) ;
#7403=LINE ( 'NONE', #37939, #28416 ) ;
#7404=DIRECTION ( 'NONE',  ( 0.7071067811865487940, -0.7071067811865463515, 0.000000000000000000 ) ) ;
#7405=ORIENTED_EDGE ( 'NONE', *, *, #48896, .F. ) ;
#7406=EDGE_LOOP ( 'NONE', ( #114356, #128447, #47214, #75460 ) ) ;
#7407=VECTOR ( 'NONE', #23376, 1000.000000000000000 ) ;
#7408=CARTESIAN_POINT ( 'NONE',  ( 5.999999999999963585, 14.96639925780211122, 5.000000000000000000 ) ) ;
#7409=DIRECTION ( 'NONE',  ( 0.7071067811865487940, 0.7071067811865463515, 0.000000000000000000 ) ) ;
#7412=EDGE_LOOP ( 'NONE', ( #72394, #102553, #137467, #29584 ) ) ;
#7413=CARTESIAN_POINT ( 'NONE',  ( -11.99451991528749417, 28.92564299267946382, 4.000000000000000000 ) ) ;
#7414=EDGE_CURVE ( 'NONE', #25495, #34714, #94745, .T. ) ;
#7416=EDGE_LOOP ( 'NONE', ( #96973, #2614, #49904, #143296 ) ) ;
#7417=DIRECTION ( 'NONE',  ( 0.7071067811865487940, 0.7071067811865463515, 0.000000000000000000 ) ) ;
#7418=VECTOR ( 'NONE', #79864, 1000.000000000000227 ) ;
#7419=DIRECTION ( 'NONE',  ( 0.6830127018922180770, -0.6830127018922204085, -0.2588190451025213501 ) ) ;
#7421=PLANE ( 'NONE',  #35664 ) ;
#7422=EDGE_LOOP ( 'NONE', ( #12684, #52595, #107687, #10267 ) ) ;
#7424=CARTESIAN_POINT ( 'NONE',  ( 9.183988606268997046, 28.73617430169793607, 5.000000000000000000 ) ) ;
#7425=AXIS2_PLACEMENT_3D ( 'NONE', #61604, #107206, #84752 ) ;
#7426=FACE_OUTER_BOUND ( 'NONE', #99400, .T. ) ;
#7427=LINE ( 'NONE', #140130, #17045 ) ;
#7428=VERTEX_POINT ( 'NONE', #106323 ) ;
#7429=FACE_OUTER_BOUND ( 'NONE', #110944, .T. ) ;
#7430=VERTEX_POINT ( 'NONE', #139738 ) ;
#7432=LINE ( 'NONE', #119064, #9958 ) ;
#7434=VERTEX_POINT ( 'NONE', #84619 ) ;
#7435=DIRECTION ( 'NONE',  ( -0.7071067811865486830, -0.7071067811865464625, 0.000000000000000000 ) ) ;
#7436=DIRECTION ( 'NONE',  ( -0.7071067811865487940, 0.7071067811865463515, 0.000000000000000000 ) ) ;
#7437=DIRECTION ( 'NONE',  ( 0.000000000000000000, 1.000000000000000000, 0.000000000000000000 ) ) ;
#7438=ADVANCED_FACE ( 'NONE', ( #7738 ), #88192, .F. ) ;
#7439=VECTOR ( 'NONE', #138530, 1000.000000000000000 ) ;
#7440=ORIENTED_EDGE ( 'NONE', *, *, #126186, .T. ) ;
#7441=CARTESIAN_POINT ( 'NONE',  ( -39.48921356237310221, -27.52281430457082934, 5.000000000000000000 ) ) ;
#7442=CARTESIAN_POINT ( 'NONE',  ( 14.51078643762690490, -27.52281430457045275, 5.000000000000000000 ) ) ;
#7443=LINE ( 'NONE', #52391, #123312 ) ;
#7444=LINE ( 'NONE', #6000, #121250 ) ;
#7445=DIRECTION ( 'NONE',  ( -0.7071067811865486830, -0.7071067811865464625, -0.000000000000000000 ) ) ;
#7446=ORIENTED_EDGE ( 'NONE', *, *, #29306, .F. ) ;
#7447=ADVANCED_FACE ( 'NONE', ( #31665 ), #32383, .T. ) ;
#7448=ORIENTED_EDGE ( 'NONE', *, *, #35784, .T. ) ;
#7449=VECTOR ( 'NONE', #80986, 1000.000000000000000 ) ;
#7450=CARTESIAN_POINT ( 'NONE',  ( 51.18398860626899705, 28.73617430169823095, 5.000000000000000000 ) ) ;
#7453=PLANE ( 'NONE',  #18056 ) ;
#7454=EDGE_CURVE ( 'NONE', #127371, #95284, #100551, .T. ) ;
#7455=DIRECTION ( 'NONE',  ( -0.000000000000000000, 0.000000000000000000, 1.000000000000000000 ) ) ;
#7457=ADVANCED_FACE ( 'NONE', ( #109925 ), #19354, .F. ) ;
#7458=ORIENTED_EDGE ( 'NONE', *, *, #114540, .T. ) ;
#7460=EDGE_CURVE ( 'NONE', #65672, #20317, #9891, .T. ) ;
#7461=CARTESIAN_POINT ( 'NONE',  ( 34.92499999999998295, -6.183345613589489531, 4.500000000000000888 ) ) ;
#7462=LINE ( 'NONE', #64020, #130366 ) ;
#7463=VECTOR ( 'NONE', #6360, 1000.000000000000000 ) ;
#7465=VECTOR ( 'NONE', #76950, 1000.000000000000000 ) ;
#7466=CARTESIAN_POINT ( 'NONE',  ( 71.99451991528749772, 28.92564299267988304, 4.000000000000000000 ) ) ;
#7467=EDGE_CURVE ( 'NONE', #142939, #4917, #77345, .T. ) ;
#7469=CARTESIAN_POINT ( 'NONE',  ( 16.00193056682086379, -22.22500000000000142, 4.500000000000000888 ) ) ;
#7470=VECTOR ( 'NONE', #68471, 1000.000000000000000 ) ;
#7472=ORIENTED_EDGE ( 'NONE', *, *, #118936, .T. ) ;
#7473=CARTESIAN_POINT ( 'NONE',  ( -18.72281430457046270, -21.72500000000000142, 5.000000000000000000 ) ) ;
#7474=ORIENTED_EDGE ( 'NONE', *, *, #37089, .F. ) ;
#7475=EDGE_CURVE ( 'NONE', #57193, #75539, #20769, .T. ) ;
#7477=VECTOR ( 'NONE', #73354, 1000.000000000000000 ) ;
#7479=CARTESIAN_POINT ( 'NONE',  ( 18.29974487139159223, -27.71228299555219010, 4.000000000000000000 ) ) ;
#7481=DIRECTION ( 'NONE',  ( -0.7071067811865486830, -0.7071067811865464625, -0.000000000000000000 ) ) ;
#7482=DIRECTION ( 'NONE',  ( 0.7071067811865487940, 0.7071067811865463515, 0.000000000000000000 ) ) ;
#7484=EDGE_CURVE ( 'NONE', #72549, #30937, #132443, .T. ) ;
#7485=DIRECTION ( 'NONE',  ( 0.3543493200069162685, -0.000000000000000000, -0.9351131265310288487 ) ) ;
#7486=ADVANCED_FACE ( 'NONE', ( #41103 ), #63606, .F. ) ;
#7487=DIRECTION ( 'NONE',  ( -0.000000000000000000, 0.3543493200069153248, 0.9351131265310292928 ) ) ;
#7488=LINE ( 'NONE', #74936, #94016 ) ;
#7490=DIRECTION ( 'NONE',  ( 0.3543493200069162685, -0.000000000000000000, -0.9351131265310288487 ) ) ;
#7492=DIRECTION ( 'NONE',  ( -0.3543493200069163240, 0.000000000000000000, 0.9351131265310288487 ) ) ;
#7494=CARTESIAN_POINT ( 'NONE',  ( 32.29289321881324071, 17.25929247661554911, 5.000000000000000000 ) ) ;
#7495=EDGE_CURVE ( 'NONE', #137044, #55653, #118661, .T. ) ;
#7498=PLANE ( 'NONE',  #22918 ) ;
#7502=CARTESIAN_POINT ( 'NONE',  ( 0.000000000000000000, 0.000000000000000000, 5.000000000000000000 ) ) ;
#7503=LINE ( 'NONE', #129285, #64798 ) ;
#7504=DIRECTION ( 'NONE',  ( 0.6830127018922181881, 0.6830127018922202975, -0.2588190451025214056 ) ) ;
#7505=VERTEX_POINT ( 'NONE', #75194 ) ;
#7506=VECTOR ( 'NONE', #38109, 1000.000000000000227 ) ;
#7507=DIRECTION ( 'NONE',  ( -0.7071067811865486830, 0.7071067811865464625, 0.000000000000000000 ) ) ;
#7510=ORIENTED_EDGE ( 'NONE', *, *, #18748, .T. ) ;
#7511=EDGE_CURVE ( 'NONE', #72734, #30899, #142576, .T. ) ;
#7512=DIRECTION ( 'NONE',  ( -0.000000000000000000, 0.3543493200069153248, 0.9351131265310292928 ) ) ;
#7514=ORIENTED_EDGE ( 'NONE', *, *, #55601, .F. ) ;
#7515=VECTOR ( 'NONE', #56621, 1000.000000000000000 ) ;
#7516=LINE ( 'NONE', #127913, #28455 ) ;
#7517=LINE ( 'NONE', #53168, #104463 ) ;
#7518=CARTESIAN_POINT ( 'NONE',  ( 9.299744871391588674, -27.71228299555212971, 4.000000000000000000 ) ) ;
#7519=DIRECTION ( 'NONE',  ( -0.7071067811865486830, -0.7071067811865464625, 0.000000000000000000 ) ) ;
#7520=PLANE ( 'NONE',  #10483 ) ;
#7523=DIRECTION ( 'NONE',  ( -0.3543493200069162685, -0.000000000000000000, -0.9351131265310288487 ) ) ;
#7525=LINE ( 'NONE', #42346, #74156 ) ;
#7526=LINE ( 'NONE', #39484, #25294 ) ;
#7527=EDGE_CURVE ( 'NONE', #49206, #120930, #140413, .T. ) ;
#7528=ORIENTED_EDGE ( 'NONE', *, *, #20157, .F. ) ;
#7529=ORIENTED_EDGE ( 'NONE', *, *, #80269, .F. ) ;
#7530=CARTESIAN_POINT ( 'NONE',  ( 57.18398860626899705, 28.73617430169827358, 5.000000000000000000 ) ) ;
#7532=FACE_OUTER_BOUND ( 'NONE', #66327, .T. ) ;
#7533=ADVANCED_FACE ( 'NONE', ( #141114 ), #85298, .F. ) ;
#7534=VECTOR ( 'NONE', #43236, 1000.000000000000227 ) ;
#7535=CARTESIAN_POINT ( 'NONE',  ( -20.29298673570681544, -21.74070752338406720, 4.999753212805217117 ) ) ;
#7537=ORIENTED_EDGE ( 'NONE', *, *, #8071, .T. ) ;
#7538=VERTEX_POINT ( 'NONE', #86041 ) ;
#7539=VECTOR ( 'NONE', #100426, 1000.000000000000000 ) ;
#7540=CARTESIAN_POINT ( 'NONE',  ( 11.70025512860841133, -27.71228299555198049, 4.000000000000000000 ) ) ;
#7543=EDGE_LOOP ( 'NONE', ( #143060, #110285, #140679, #17538 ) ) ;
#7544=EDGE_CURVE ( 'NONE', #97811, #60787, #141872, .T. ) ;
#7545=DIRECTION ( 'NONE',  ( -0.7071067811865486830, -0.7071067811865464625, -0.000000000000000000 ) ) ;
#7547=LINE ( 'NONE', #108999, #110465 ) ;
#7549=FACE_OUTER_BOUND ( 'NONE', #135720, .T. ) ;
#7550=EDGE_CURVE ( 'NONE', #116840, #20377, #42567, .T. ) ;
#7551=FACE_BOUND ( 'NONE', #34431, .T. ) ;
#7552=CARTESIAN_POINT ( 'NONE',  ( -69.18398860626899705, 28.73617430169835529, 5.000000000000000000 ) ) ;
#7553=CARTESIAN_POINT ( 'NONE',  ( 21.32816939922338406, -9.740707523384177335, 4.000000000000000000 ) ) ;
#7555=CARTESIAN_POINT ( 'NONE',  ( -34.92500000000001137, -4.298069433178936194, 4.500000000000000888 ) ) ;
#7556=DIRECTION ( 'NONE',  ( 4.681814790819592407E-17, 0.3543493200069153248, 0.9351131265310292928 ) ) ;
#7557=VERTEX_POINT ( 'NONE', #86767 ) ;
#7560=ORIENTED_EDGE ( 'NONE', *, *, #106648, .T. ) ;
#7561=ORIENTED_EDGE ( 'NONE', *, *, #107033, .T. ) ;
#7563=EDGE_LOOP ( 'NONE', ( #32025, #104865, #36140, #57891 ) ) ;
#7564=CARTESIAN_POINT ( 'NONE',  ( 29.20710678118633652, 15.75929247661555443, 5.000000000000000000 ) ) ;
#7565=FACE_OUTER_BOUND ( 'NONE', #103019, .T. ) ;
#7567=VECTOR ( 'NONE', #129232, 1000.000000000000227 ) ;
#7569=VECTOR ( 'NONE', #13633, 999.9999999999998863 ) ;
#7570=CARTESIAN_POINT ( 'NONE',  ( -1.499999999999987566, -17.91344420646042934, 1.358650452708460854 ) ) ;
#7571=DIRECTION ( 'NONE',  ( 0.7071067811865487940, -0.7071067811865463515, 0.000000000000000000 ) ) ;
#7573=DIRECTION ( 'NONE',  ( 0.7071067811865487940, 0.7071067811865463515, 0.000000000000000000 ) ) ;
#7574=CARTESIAN_POINT ( 'NONE',  ( -32.67183060077623935, -3.740707523384244837, 4.000000000000000000 ) ) ;
#7575=CARTESIAN_POINT ( 'NONE',  ( -16.82816939922340893, 18.75929247661553134, 4.000000000000000000 ) ) ;
#7576=DIRECTION ( 'NONE',  ( 0.7071067811865487940, 0.7071067811865463515, 0.000000000000000000 ) ) ;
#7577=PLANE ( 'NONE',  #43950 ) ;
#7578=VECTOR ( 'NONE', #52367, 1000.000000000000000 ) ;
#7579=VECTOR ( 'NONE', #77450, 1000.000000000000000 ) ;
#7581=DIRECTION ( 'NONE',  ( -0.7071067811865486830, -0.7071067811865464625, -0.000000000000000000 ) ) ;
#7582=ORIENTED_EDGE ( 'NONE', *, *, #1854, .T. ) ;
#7583=CARTESIAN_POINT ( 'NONE',  ( 38.99451991528749062, 28.92564299267965211, 4.000000000000000000 ) ) ;
#7584=LINE ( 'NONE', #20604, #104447 ) ;
#7585=ORIENTED_EDGE ( 'NONE', *, *, #76580, .F. ) ;
#7586=ORIENTED_EDGE ( 'NONE', *, *, #30309, .T. ) ;
#7587=ADVANCED_FACE ( 'NONE', ( #101186 ), #12031, .F. ) ;
#7588=ORIENTED_EDGE ( 'NONE', *, *, #129288, .T. ) ;
#7591=DIRECTION ( 'NONE',  ( 0.7071067811865487940, 0.7071067811865463515, 0.000000000000000000 ) ) ;
#7592=VECTOR ( 'NONE', #121405, 1000.000000000000000 ) ;
#7595=VERTEX_POINT ( 'NONE', #13441 ) ;
#7596=CARTESIAN_POINT ( 'NONE',  ( 36.18398860626899705, 28.73617430169812437, 5.000000000000000000 ) ) ;
#7597=ORIENTED_EDGE ( 'NONE', *, *, #93848, .F. ) ;
#7598=PLANE ( 'NONE',  #78941 ) ;
#7599=DIRECTION ( 'NONE',  ( -1.000000000000000000, 0.000000000000000000, -0.000000000000000000 ) ) ;
#7600=CARTESIAN_POINT ( 'NONE',  ( 9.299744871391588674, -27.71228299555212971, 4.000000000000000000 ) ) ;
#7601=ORIENTED_EDGE ( 'NONE', *, *, #20023, .T. ) ;
#7602=VERTEX_POINT ( 'NONE', #102643 ) ;
#7603=EDGE_CURVE ( 'NONE', #125282, #62063, #70046, .T. ) ;
#7604=DIRECTION ( 'NONE',  ( -0.7071067811865486830, -0.7071067811865464625, 0.000000000000000000 ) ) ;
#7605=VECTOR ( 'NONE', #41858, 999.9999999999998863 ) ;
#7606=ORIENTED_EDGE ( 'NONE', *, *, #6615, .T. ) ;
#7607=LINE ( 'NONE', #13315, #119864 ) ;
#7608=VERTEX_POINT ( 'NONE', #45423 ) ;
#7610=ORIENTED_EDGE ( 'NONE', *, *, #84921, .F. ) ;
#7611=VECTOR ( 'NONE', #127844, 1000.000000000000000 ) ;
#7612=EDGE_LOOP ( 'NONE', ( #38070, #57452, #10904, #31312 ) ) ;
#7614=LINE ( 'NONE', #119237, #53810 ) ;
#7615=CARTESIAN_POINT ( 'NONE',  ( 34.47516574401891631, 0.02806734111581514132, 4.998110765256834398 ) ) ;
#7616=DIRECTION ( 'NONE',  ( -0.7071067811865486830, -0.7071067811865464625, 0.000000000000000000 ) ) ;
#7617=DIRECTION ( 'NONE',  ( -0.7071067811865487940, 0.7071067811865463515, -0.000000000000000000 ) ) ;
#7619=LINE ( 'NONE', #140301, #90475 ) ;
#7620=ORIENTED_EDGE ( 'NONE', *, *, #139462, .T. ) ;
#7621=DIRECTION ( 'NONE',  ( 0.6830127018922180770, -0.6830127018922204085, -0.2588190451025213501 ) ) ;
#7622=AXIS2_PLACEMENT_3D ( 'NONE', #98586, #142815, #41344 ) ;
#7624=LINE ( 'NONE', #10309, #113355 ) ;
#7625=EDGE_CURVE ( 'NONE', #84565, #129451, #56316, .T. ) ;
#7627=CARTESIAN_POINT ( 'NONE',  ( -51.29974487139158867, -27.71228299555242103, 4.000000000000000000 ) ) ;
#7628=CARTESIAN_POINT ( 'NONE',  ( -30.32816939922330945, 5.259292476615672562, 4.000000000000000000 ) ) ;
#7629=ORIENTED_EDGE ( 'NONE', *, *, #57360, .T. ) ;
#7630=EDGE_CURVE ( 'NONE', #130905, #110484, #99761, .T. ) ;
#7631=ORIENTED_EDGE ( 'NONE', *, *, #11156, .T. ) ;
#7632=VECTOR ( 'NONE', #125080, 1000.000000000000000 ) ;
#7634=CARTESIAN_POINT ( 'NONE',  ( -48.48921356237309510, -27.52281430457089328, 5.000000000000000000 ) ) ;
#7635=DIRECTION ( 'NONE',  ( -0.6830127018922180770, -0.6830127018922204085, -0.2588190451025213501 ) ) ;
#7636=DIRECTION ( 'NONE',  ( -0.7071067811865487940, 0.7071067811865463515, -0.000000000000000000 ) ) ;
#7637=AXIS2_PLACEMENT_3D ( 'NONE', #26080, #92734, #128251 ) ;
#7638=DIRECTION ( 'NONE',  ( -0.3543493200069162685, -0.000000000000000000, -0.9351131265310288487 ) ) ;
#7640=EDGE_CURVE ( 'NONE', #77421, #129881, #80190, .T. ) ;
#7642=ADVANCED_FACE ( 'NONE', ( #23633 ), #78741, .F. ) ;
#7643=( BOUNDED_CURVE ( )  B_SPLINE_CURVE ( 3, ( #20874, #109329, #44087, #41206 ),
 .UNSPECIFIED., .F., .F. ) 
 B_SPLINE_CURVE_WITH_KNOTS ( ( 4, 4 ),
 ( 1.208578181583236821, 1.359146454359482892 ),
 .UNSPECIFIED. ) 
 CURVE ( )  GEOMETRIC_REPRESENTATION_ITEM ( )  RATIONAL_B_SPLINE_CURVE ( ( 1.000000000000000000, 0.9981116584018941973, 0.9981116584018941973, 1.000000000000000000 ) ) 
 REPRESENTATION_ITEM ( '' )  );
#7645=CARTESIAN_POINT ( 'NONE',  ( -25.49999999999982236, -2.947814304570797184, 5.000000000000000000 ) ) ;
#7646=DIRECTION ( 'NONE',  ( -0.000000000000000000, 0.3543493200069153248, 0.9351131265310292928 ) ) ;
#7649=CARTESIAN_POINT ( 'NONE',  ( -17.82446237275610201, 9.017796866808286183, 4.672399651904014739 ) ) ;
#7650=ORIENTED_EDGE ( 'NONE', *, *, #17910, .F. ) ;
#7652=LINE ( 'NONE', #48496, #119516 ) ;
#7653=DIRECTION ( 'NONE',  ( -0.6830127018922180770, -0.6830127018922204085, -0.2588190451025213501 ) ) ;
#7654=ORIENTED_EDGE ( 'NONE', *, *, #95997, .F. ) ;
#7655=( BOUNDED_CURVE ( )  B_SPLINE_CURVE ( 3, ( #34854, #14505, #124695, #135590 ),
 .UNSPECIFIED., .F., .F. ) 
 B_SPLINE_CURVE_WITH_KNOTS ( ( 4, 4 ),
 ( 5.106027341939272546, 6.645403452391245303 ),
 .UNSPECIFIED. ) 
 CURVE ( )  GEOMETRIC_REPRESENTATION_ITEM ( )  RATIONAL_B_SPLINE_CURVE ( ( 1.000000000000000000, 0.8120851936182260644, 0.8120851936182260644, 1.000000000000000000 ) ) 
 REPRESENTATION_ITEM ( '' )  );
#7656=LINE ( 'NONE', #117131, #120198 ) ;
#7657=CARTESIAN_POINT ( 'NONE',  ( -34.49999999999974420, -17.94567065516885762, 4.994342998332165884 ) ) ;
#7658=VERTEX_POINT ( 'NONE', #133831 ) ;
#7660=ADVANCED_FACE ( 'NONE', ( #123692 ), #57717, .T. ) ;
#7661=DIRECTION ( 'NONE',  ( 1.000000000000000000, 0.000000000000000000, 0.000000000000000000 ) ) ;
#7663=ORIENTED_EDGE ( 'NONE', *, *, #89794, .F. ) ;
#7664=VECTOR ( 'NONE', #126113, 999.9999999999998863 ) ;
#7668=CARTESIAN_POINT ( 'NONE',  ( -24.18398860626899705, 28.73617430169804265, 5.000000000000000000 ) ) ;
#7669=EDGE_CURVE ( 'NONE', #64185, #81832, #33817, .T. ) ;
#7671=CARTESIAN_POINT ( 'NONE',  ( 9.792893218813391698, -11.24070752338417201, 5.000000000000000000 ) ) ;
#7672=CARTESIAN_POINT ( 'NONE',  ( 34.75611968250419181, -10.29434930147584737, 4.955485411084881164 ) ) ;
#7673=ORIENTED_EDGE ( 'NONE', *, *, #37426, .F. ) ;
#7674=DIRECTION ( 'NONE',  ( -0.7071067811865487940, 0.7071067811865463515, -0.000000000000000000 ) ) ;
#7675=CARTESIAN_POINT ( 'NONE',  ( 24.79333936457830134, 21.75929247661549226, 4.998822639870711626 ) ) ;
#7677=EDGE_CURVE ( 'NONE', #10831, #136292, #112090, .T. ) ;
#7678=CARTESIAN_POINT ( 'NONE',  ( 1.001930566820972812, -22.22500000000000142, 4.500000000000000888 ) ) ;
#7679=ORIENTED_EDGE ( 'NONE', *, *, #62664, .T. ) ;
#7680=VECTOR ( 'NONE', #110991, 1000.000000000000227 ) ;
#7681=CARTESIAN_POINT ( 'NONE',  ( -18.18398860626898994, 28.73617430169800002, 5.000000000000000000 ) ) ;
#7682=ORIENTED_EDGE ( 'NONE', *, *, #128705, .T. ) ;
#7684=FACE_OUTER_BOUND ( 'NONE', #66904, .T. ) ;
#7685=ADVANCED_FACE ( 'NONE', ( #3290 ), #78038, .F. ) ;
#7687=CARTESIAN_POINT ( 'NONE',  ( -32.99999999999977263, -2.904428200921339354, -6.989807076074864511 ) ) ;
#7689=ORIENTED_EDGE ( 'NONE', *, *, #140447, .T. ) ;
#7690=FACE_OUTER_BOUND ( 'NONE', #19599, .T. ) ;
#7691=AXIS2_PLACEMENT_3D ( 'NONE', #71116, #49376, #60239 ) ;
#7692=CARTESIAN_POINT ( 'NONE',  ( 31.49999999999977973, 22.01701374228158059, 2.453858888625559231 ) ) ;
#7693=CARTESIAN_POINT ( 'NONE',  ( 27.18398860626900060, 28.73617430169806042, 5.000000000000000000 ) ) ;
#7694=CARTESIAN_POINT ( 'NONE',  ( -14.56453960929607128, -0.7633378608190106718, 4.223415947001583959 ) ) ;
#7695=ORIENTED_EDGE ( 'NONE', *, *, #54600, .T. ) ;
#7696=DIRECTION ( 'NONE',  ( 0.7071067811865487940, 0.7071067811865463515, 0.000000000000000000 ) ) ;
#7700=ORIENTED_EDGE ( 'NONE', *, *, #105022, .F. ) ;
#7701=EDGE_CURVE ( 'NONE', #93695, #25745, #34513, .T. ) ;
#7702=ORIENTED_EDGE ( 'NONE', *, *, #78552, .T. ) ;
#7705=ORIENTED_EDGE ( 'NONE', *, *, #115101, .T. ) ;
#7706=FACE_OUTER_BOUND ( 'NONE', #28715, .T. ) ;
#7708=CARTESIAN_POINT ( 'NONE',  ( 33.29974487139158867, -27.71228299555229313, 4.000000000000000000 ) ) ;
#7710=VERTEX_POINT ( 'NONE', #47576 ) ;
#7712=CARTESIAN_POINT ( 'NONE',  ( 36.29974487139159578, -27.71228299555231445, 4.000000000000000000 ) ) ;
#7713=VECTOR ( 'NONE', #122807, 1000.000000000000114 ) ;
#7715=AXIS2_PLACEMENT_3D ( 'NONE', #14527, #68243, #113111 ) ;
#7716=EDGE_CURVE ( 'NONE', #134224, #88846, #12739, .T. ) ;
#7717=PLANE ( 'NONE',  #69869 ) ;
#7719=DIRECTION ( 'NONE',  ( -0.6830127018922181881, 0.6830127018922202975, -0.2588190451025214056 ) ) ;
#7721=VECTOR ( 'NONE', #102528, 1000.000000000000000 ) ;
#7722=ORIENTED_EDGE ( 'NONE', *, *, #12563, .F. ) ;
#7723=EDGE_CURVE ( 'NONE', #61774, #140269, #90312, .T. ) ;
#7724=FACE_BOUND ( 'NONE', #57182, .T. ) ;
#7725=DIRECTION ( 'NONE',  ( 0.3543493200069162685, -0.000000000000000000, -0.9351131265310288487 ) ) ;
#7726=DIRECTION ( 'NONE',  ( -0.7071067811865486830, -0.7071067811865464625, 0.000000000000000000 ) ) ;
#7727=CYLINDRICAL_SURFACE ( 'NONE', #82768, 0.5000000000000004441 ) ;
#7728=VECTOR ( 'NONE', #67904, 1000.000000000000000 ) ;
#7730=ORIENTED_EDGE ( 'NONE', *, *, #124158, .T. ) ;
#7731=VECTOR ( 'NONE', #141753, 1000.000000000000227 ) ;
#7732=ORIENTED_EDGE ( 'NONE', *, *, #135394, .T. ) ;
#7733=ORIENTED_EDGE ( 'NONE', *, *, #80802, .T. ) ;
#7734=ORIENTED_EDGE ( 'NONE', *, *, #61915, .F. ) ;
#7735=AXIS2_PLACEMENT_3D ( 'NONE', #137526, #59280, #4799 ) ;
#7737=DIRECTION ( 'NONE',  ( -0.7071067811865486830, -0.7071067811865464625, 0.000000000000000000 ) ) ;
#7738=FACE_OUTER_BOUND ( 'NONE', #44858, .T. ) ;
#7739=ORIENTED_EDGE ( 'NONE', *, *, #122105, .F. ) ;
#7740=DIRECTION ( 'NONE',  ( 0.7071067811865487940, 0.7071067811865463515, -0.000000000000000000 ) ) ;
#7741=LINE ( 'NONE', #76623, #79776 ) ;
#7742=EDGE_CURVE ( 'NONE', #92118, #78177, #91062, .T. ) ;
#7743=LINE ( 'NONE', #96176, #73525 ) ;
#7744=DIRECTION ( 'NONE',  ( -0.000000000000000000, -0.000000000000000000, 1.000000000000000000 ) ) ;
#7747=ORIENTED_EDGE ( 'NONE', *, *, #24735, .T. ) ;
#7750=EDGE_LOOP ( 'NONE', ( #114604, #82815, #61346, #128148 ) ) ;
#7751=EDGE_CURVE ( 'NONE', #32796, #72863, #135283, .T. ) ;
#7752=CARTESIAN_POINT ( 'NONE',  ( -34.75611968250420603, 20.81293425470715519, 4.955485411084898040 ) ) ;
#7753=ORIENTED_EDGE ( 'NONE', *, *, #21670, .F. ) ;
#7754=FACE_OUTER_BOUND ( 'NONE', #7785, .T. ) ;
#7755=EDGE_CURVE ( 'NONE', #96557, #93700, #93879, .T. ) ;
#7756=ORIENTED_EDGE ( 'NONE', *, *, #44182, .F. ) ;
#7759=VERTEX_POINT ( 'NONE', #14890 ) ;
#7760=ORIENTED_EDGE ( 'NONE', *, *, #117657, .F. ) ;
#7761=CARTESIAN_POINT ( 'NONE',  ( -34.42500000000001137, -7.458600742197909916, 5.000000000000000000 ) ) ;
#7762=ADVANCED_FACE ( 'NONE', ( #81614 ), #60586, .F. ) ;
#7763=AXIS2_PLACEMENT_3D ( 'NONE', #60790, #83215, #104951 ) ;
#7764=CARTESIAN_POINT ( 'NONE',  ( -32.99999999999977263, 1.761378380278653344, -6.096875308897330648 ) ) ;
#7766=EDGE_CURVE ( 'NONE', #120604, #47491, #17723, .T. ) ;
#7767=DIRECTION ( 'NONE',  ( 1.000000000000000000, 0.000000000000000000, 0.000000000000000000 ) ) ;
#7768=DIRECTION ( 'NONE',  ( -0.7071067811865487940, 0.7071067811865463515, 0.000000000000000000 ) ) ;
#7769=DIRECTION ( 'NONE',  ( -0.6830127018922181881, 0.6830127018922202975, -0.2588190451025214056 ) ) ;
#7770=CARTESIAN_POINT ( 'NONE',  ( -54.29974487139159578, -27.71228299555243879, 4.000000000000000000 ) ) ;
#7771=EDGE_CURVE ( 'NONE', #70901, #70593, #37375, .T. ) ;
#7772=AXIS2_PLACEMENT_3D ( 'NONE', #89803, #55779, #56526 ) ;
#7773=LINE ( 'NONE', #120824, #102307 ) ;
#7774=LINE ( 'NONE', #129562, #116916 ) ;
#7775=VERTEX_POINT ( 'NONE', #26495 ) ;
#7778=ORIENTED_EDGE ( 'NONE', *, *, #37463, .F. ) ;
#7779=ORIENTED_EDGE ( 'NONE', *, *, #81065, .T. ) ;
#7780=ORIENTED_EDGE ( 'NONE', *, *, #26217, .T. ) ;
#7781=EDGE_LOOP ( 'NONE', ( #123137, #2024, #58597, #97637 ) ) ;
#7782=LINE ( 'NONE', #73094, #134749 ) ;
#7783=FACE_OUTER_BOUND ( 'NONE', #3489, .T. ) ;
#7784=CARTESIAN_POINT ( 'NONE',  ( 6.707106781186501721, -0.7407075233842770334, 5.000000000000000000 ) ) ;
#7785=EDGE_LOOP ( 'NONE', ( #14242, #138122, #111563, #82137 ) ) ;
#7787=VERTEX_POINT ( 'NONE', #61315 ) ;
#7788=VECTOR ( 'NONE', #14367, 999.9999999999998863 ) ;
#7789=VECTOR ( 'NONE', #47150, 1000.000000000000000 ) ;
#7791=DIRECTION ( 'NONE',  ( -0.7071067811865486830, -0.7071067811865464625, 0.000000000000000000 ) ) ;
#7792=EDGE_CURVE ( 'NONE', #1886, #40019, #59162, .T. ) ;
#7793=PLANE ( 'NONE',  #122359 ) ;
#7794=CARTESIAN_POINT ( 'NONE',  ( 34.49999999999975131, 9.054329344830847504, 4.994342998332164107 ) ) ;
#7795=ORIENTED_EDGE ( 'NONE', *, *, #111759, .F. ) ;
#7797=VERTEX_POINT ( 'NONE', #128659 ) ;
#7798=ORIENTED_EDGE ( 'NONE', *, *, #133031, .F. ) ;
#7799=CARTESIAN_POINT ( 'NONE',  ( 0.000000000000000000, 0.000000000000000000, 5.000000000000000000 ) ) ;
#7801=DIRECTION ( 'NONE',  ( -0.7071067811865486830, -0.7071067811865464625, 0.000000000000000000 ) ) ;
#7803=AXIS2_PLACEMENT_3D ( 'NONE', #62563, #49568, #50260 ) ;
#7804=PLANE ( 'NONE',  #106104 ) ;
#7805=EDGE_CURVE ( 'NONE', #106932, #35816, #93175, .T. ) ;
#7806=EDGE_CURVE ( 'NONE', #70774, #125073, #29331, .T. ) ;
#7807=CARTESIAN_POINT ( 'NONE',  ( -36.29974487139159578, -27.71228299555231445, 4.000000000000000000 ) ) ;
#7808=DIRECTION ( 'NONE',  ( 0.7071067811865487940, 0.7071067811865463515, 0.000000000000000000 ) ) ;
#7809=DIRECTION ( 'NONE',  ( -0.7071067811865486830, 0.7071067811865464625, 0.000000000000000000 ) ) ;
#7810=VECTOR ( 'NONE', #71141, 1000.000000000000000 ) ;
#7813=CARTESIAN_POINT ( 'NONE',  ( -17.99451991528748351, 28.92564299267950645, 4.000000000000000000 ) ) ;
#7814=VERTEX_POINT ( 'NONE', #28652 ) ;
#7815=CARTESIAN_POINT ( 'NONE',  ( 11.51078643762690490, -27.52281430457047406, 5.000000000000000000 ) ) ;
#7816=CARTESIAN_POINT ( 'NONE',  ( -23.79027397808395250, -22.22500000000000142, 9.219363927620312538 ) ) ;
#7817=EDGE_LOOP ( 'NONE', ( #25721, #109358, #12975, #18997 ) ) ;
#7819=CARTESIAN_POINT ( 'NONE',  ( 27.18398860626900060, 28.73617430169806042, 5.000000000000000000 ) ) ;
#7821=VERTEX_POINT ( 'NONE', #72905 ) ;
#7822=ADVANCED_FACE ( 'NONE', ( #62001 ), #106157, .F. ) ;
#7823=VECTOR ( 'NONE', #115282, 1000.000000000000000 ) ;
#7824=EDGE_CURVE ( 'NONE', #28405, #12698, #116354, .T. ) ;
#7825=CARTESIAN_POINT ( 'NONE',  ( 15.29974487139158867, -27.71228299555216879, 4.000000000000000000 ) ) ;
#7826=LINE ( 'NONE', #73820, #62400 ) ;
#7827=ORIENTED_EDGE ( 'NONE', *, *, #39811, .T. ) ;
#7828=CARTESIAN_POINT ( 'NONE',  ( -19.40370036533107978, 9.134293891043357760, 4.529189151624868792 ) ) ;
#7829=ORIENTED_EDGE ( 'NONE', *, *, #34468, .T. ) ;
#7831=VECTOR ( 'NONE', #119538, 1000.000000000000000 ) ;
#7832=CARTESIAN_POINT ( 'NONE',  ( -16.49999999999988276, -2.568876922607790103, 4.000000000000000000 ) ) ;
#7834=CARTESIAN_POINT ( 'NONE',  ( 7.499999999999954703, 13.08746187583911080, 4.000000000000000000 ) ) ;
#7836=EDGE_CURVE ( 'NONE', #80414, #99670, #92430, .T. ) ;
#7837=DIRECTION ( 'NONE',  ( -0.6830127018922180770, -0.6830127018922204085, -0.2588190451025213501 ) ) ;
#7838=CARTESIAN_POINT ( 'NONE',  ( -1.968364840778075830, 2.259292476615697876, 13.77329220150636679 ) ) ;
#7839=DIRECTION ( 'NONE',  ( -0.3543493200069162685, -0.000000000000000000, -0.9351131265310288487 ) ) ;
#7842=VECTOR ( 'NONE', #140337, 1000.000000000000000 ) ;
#7844=CARTESIAN_POINT ( 'NONE',  ( 0.000000000000000000, 0.000000000000000000, 5.000000000000000000 ) ) ;
#7845=FACE_OUTER_BOUND ( 'NONE', #99963, .T. ) ;
#7846=ORIENTED_EDGE ( 'NONE', *, *, #46607, .F. ) ;
#7847=EDGE_LOOP ( 'NONE', ( #125342, #6942, #130844, #99135 ) ) ;
#7848=DIRECTION ( 'NONE',  ( 0.000000000000000000, 0.000000000000000000, 1.000000000000000000 ) ) ;
#7850=DIRECTION ( 'NONE',  ( 0.7071067811865486830, -0.7071067811865464625, -0.000000000000000000 ) ) ;
#7851=DIRECTION ( 'NONE',  ( -0.7071067811865486830, -0.7071067811865464625, 0.000000000000000000 ) ) ;
#7852=AXIS2_PLACEMENT_3D ( 'NONE', #51344, #60824, #86106 ) ;
#7854=CARTESIAN_POINT ( 'NONE',  ( 9.489213562373095101, -27.52281430457062328, 5.000000000000000000 ) ) ;
#7855=ORIENTED_EDGE ( 'NONE', *, *, #65775, .F. ) ;
#7856=CARTESIAN_POINT ( 'NONE',  ( 54.18398860626899705, 28.73617430169825226, 5.000000000000000000 ) ) ;
#7857=LINE ( 'NONE', #107871, #81325 ) ;
#7858=DIRECTION ( 'NONE',  ( -0.7071067811865487940, 0.7071067811865463515, -0.000000000000000000 ) ) ;
#7859=CARTESIAN_POINT ( 'NONE',  ( 15.48921356237309510, -27.52281430457066236, 5.000000000000000000 ) ) ;
#7860=CARTESIAN_POINT ( 'NONE',  ( 22.49999999999984368, 12.43112307739206024, 4.000000000000000000 ) ) ;
#7861=ORIENTED_EDGE ( 'NONE', *, *, #134555, .F. ) ;
#7862=EDGE_CURVE ( 'NONE', #33632, #30495, #104012, .T. ) ;
#7863=CARTESIAN_POINT ( 'NONE',  ( -27.48921356237309155, -27.52281430457074762, 5.000000000000000000 ) ) ;
#7864=DIRECTION ( 'NONE',  ( 0.7071067811865487940, -0.7071067811865463515, 0.000000000000000000 ) ) ;
#7865=FACE_OUTER_BOUND ( 'NONE', #45675, .T. ) ;
#7866=PLANE ( 'NONE',  #1196 ) ;
#7868=ORIENTED_EDGE ( 'NONE', *, *, #78693, .T. ) ;
#7869=EDGE_CURVE ( 'NONE', #109630, #139077, #139572, .T. ) ;
#7870=ORIENTED_EDGE ( 'NONE', *, *, #96785, .F. ) ;
#7871=VERTEX_POINT ( 'NONE', #50396 ) ;
#7873=VECTOR ( 'NONE', #82886, 1000.000000000000000 ) ;
#7875=CARTESIAN_POINT ( 'NONE',  ( 21.52400138585433709, 22.03583458319438293, 4.979811245910091166 ) ) ;
#7876=CARTESIAN_POINT ( 'NONE',  ( -48.18398860626899705, 28.73617430169820608, 5.000000000000000000 ) ) ;
#7877=ORIENTED_EDGE ( 'NONE', *, *, #85540, .T. ) ;
#7878=ADVANCED_FACE ( 'NONE', ( #38099 ), #40255, .F. ) ;
#7879=PLANE ( 'NONE',  #134773 ) ;
#7880=LINE ( 'NONE', #84753, #76770 ) ;
#7881=VECTOR ( 'NONE', #94415, 1000.000000000000000 ) ;
#7884=DIRECTION ( 'NONE',  ( 0.6830127018922180770, -0.6830127018922204085, -0.2588190451025213501 ) ) ;
#7885=PLANE ( 'NONE',  #117069 ) ;
#7886=CARTESIAN_POINT ( 'NONE',  ( -24.79333936457829779, 21.75929247661549581, 4.998822639870701856 ) ) ;
#7887=DIRECTION ( 'NONE',  ( -0.7071067811865487940, 0.7071067811865463515, -0.000000000000000000 ) ) ;
#7891=DIRECTION ( 'NONE',  ( -0.3543493200069162685, -0.000000000000000000, -0.9351131265310288487 ) ) ;
#7892=CARTESIAN_POINT ( 'NONE',  ( 31.49999999999979039, -7.912538124160673370, 4.000000000000000000 ) ) ;
#7894=AXIS2_PLACEMENT_3D ( 'NONE', #67916, #57728, #33144 ) ;
#7895=LINE ( 'NONE', #130431, #85024 ) ;
#7897=VECTOR ( 'NONE', #44825, 999.9999999999998863 ) ;
#7899=ORIENTED_EDGE ( 'NONE', *, *, #59113, .T. ) ;
#7900=VECTOR ( 'NONE', #6208, 1000.000000000000114 ) ;
#7901=CARTESIAN_POINT ( 'NONE',  ( 24.18398860626899705, 28.73617430169804265, 5.000000000000000000 ) ) ;
#7903=EDGE_CURVE ( 'NONE', #138539, #44911, #16290, .T. ) ;
#7904=ORIENTED_EDGE ( 'NONE', *, *, #127521, .T. ) ;
#7906=CARTESIAN_POINT ( 'NONE',  ( -60.48921356237309510, -27.52281430457097500, 5.000000000000000000 ) ) ;
#7907=ORIENTED_EDGE ( 'NONE', *, *, #61365, .T. ) ;
#7909=CARTESIAN_POINT ( 'NONE',  ( 0.000000000000000000, 0.000000000000000000, 5.000000000000000000 ) ) ;
#7910=EDGE_CURVE ( 'NONE', #16291, #20377, #109027, .T. ) ;
#7911=LINE ( 'NONE', #50030, #59475 ) ;
#7912=CARTESIAN_POINT ( 'NONE',  ( 36.18398860626899705, 28.73617430169812437, 5.000000000000000000 ) ) ;
#7914=ORIENTED_EDGE ( 'NONE', *, *, #7986, .T. ) ;
#7915=DIRECTION ( 'NONE',  ( 0.7071067811865486830, -0.7071067811865464625, -0.000000000000000000 ) ) ;
#7916=CARTESIAN_POINT ( 'NONE',  ( -8.206660635421469507, 21.75929247661548516, 4.998822639870715179 ) ) ;
#7917=VECTOR ( 'NONE', #36015, 1000.000000000000000 ) ;
#7918=ORIENTED_EDGE ( 'NONE', *, *, #34544, .T. ) ;
#7920=EDGE_CURVE ( 'NONE', #137750, #102574, #10025, .T. ) ;
#7922=ORIENTED_EDGE ( 'NONE', *, *, #80131, .F. ) ;
#7924=EDGE_CURVE ( 'NONE', #13610, #122891, #32208, .T. ) ;
#7926=ORIENTED_EDGE ( 'NONE', *, *, #50869, .F. ) ;
#7927=ORIENTED_EDGE ( 'NONE', *, *, #130387, .T. ) ;
#7928=VECTOR ( 'NONE', #54382, 999.9999999999998863 ) ;
#7929=ADVANCED_FACE ( 'NONE', ( #141690 ), #63440, .T. ) ;
#7930=PLANE ( 'NONE',  #7181 ) ;
#7931=VECTOR ( 'NONE', #3158, 1000.000000000000000 ) ;
#7932=AXIS2_PLACEMENT_3D ( 'NONE', #7250, #42080, #41326 ) ;
#7933=DIRECTION ( 'NONE',  ( -0.7071067811865486830, -0.7071067811865464625, -0.000000000000000000 ) ) ;
#7934=PLANE ( 'NONE',  #86625 ) ;
#7937=EDGE_CURVE ( 'NONE', #118585, #103206, #130099, .T. ) ;
#7938=DIRECTION ( 'NONE',  ( 0.6830127018922180770, -0.6830127018922204085, -0.2588190451025213501 ) ) ;
#7939=CARTESIAN_POINT ( 'NONE',  ( -22.49999999999984723, -14.94781430457067195, 5.000000000000000000 ) ) ;
#7942=DIRECTION ( 'NONE',  ( -0.7071067811865486830, -0.7071067811865464625, 0.000000000000000000 ) ) ;
#7943=FACE_OUTER_BOUND ( 'NONE', #3747, .T. ) ;
#7944=CARTESIAN_POINT ( 'NONE',  ( 34.92499999999998295, -21.72500000000000142, 5.000000000000000000 ) ) ;
#7945=ORIENTED_EDGE ( 'NONE', *, *, #49468, .T. ) ;
#7946=ORIENTED_EDGE ( 'NONE', *, *, #108964, .F. ) ;
#7947=ORIENTED_EDGE ( 'NONE', *, *, #124276, .F. ) ;
#7948=EDGE_LOOP ( 'NONE', ( #96073, #52877, #84012, #18772 ) ) ;
#7950=EDGE_CURVE ( 'NONE', #139004, #127787, #143102, .T. ) ;
#7951=ORIENTED_EDGE ( 'NONE', *, *, #136975, .T. ) ;
#7952=ORIENTED_EDGE ( 'NONE', *, *, #129255, .F. ) ;
#7953=LINE ( 'NONE', #31175, #120832 ) ;
#7955=DIRECTION ( 'NONE',  ( -0.7071067811865487940, 0.7071067811865463515, -0.000000000000000000 ) ) ;
#7956=EDGE_LOOP ( 'NONE', ( #97977, #83457, #5561, #108629 ) ) ;
#7957=CARTESIAN_POINT ( 'NONE',  ( 14.99999999999989697, -18.03360074219755660, 5.000000000000000000 ) ) ;
#7959=ORIENTED_EDGE ( 'NONE', *, *, #47900, .T. ) ;
#7961=CARTESIAN_POINT ( 'NONE',  ( -11.01088028653940576, -22.02621442084247860, 4.990779571109222879 ) ) ;
#7963=ORIENTED_EDGE ( 'NONE', *, *, #70023, .T. ) ;
#7965=DIRECTION ( 'NONE',  ( -0.3543493200069162685, -0.000000000000000000, -0.9351131265310288487 ) ) ;
#7966=PLANE ( 'NONE',  #14226 ) ;
#7967=CARTESIAN_POINT ( 'NONE',  ( -11.29289321881336861, -12.74070752338415247, 5.000000000000000000 ) ) ;
#7968=ORIENTED_EDGE ( 'NONE', *, *, #10546, .F. ) ;
#7970=VERTEX_POINT ( 'NONE', #52515 ) ;
#7971=FACE_OUTER_BOUND ( 'NONE', #46397, .T. ) ;
#7972=VERTEX_POINT ( 'NONE', #120608 ) ;
#7974=CARTESIAN_POINT ( 'NONE',  ( 9.516654386410381861, 22.22500000000000142, 4.500000000000000888 ) ) ;
#7975=CARTESIAN_POINT ( 'NONE',  ( -11.99999999999991651, 7.931123077392104648, 4.000000000000000000 ) ) ;
#7976=LINE ( 'NONE', #63829, #81967 ) ;
#7977=VECTOR ( 'NONE', #94245, 1000.000000000000000 ) ;
#7978=VERTEX_POINT ( 'NONE', #109757 ) ;
#7979=EDGE_CURVE ( 'NONE', #108003, #35148, #142410, .T. ) ;
#7980=EDGE_CURVE ( 'NONE', #29089, #122015, #20591, .T. ) ;
#7981=PLANE ( 'NONE',  #90071 ) ;
#7982=PLANE ( 'NONE',  #56147 ) ;
#7984=DIRECTION ( 'NONE',  ( 1.000000000000000000, 0.000000000000000000, 0.000000000000000000 ) ) ;
#7985=PLANE ( 'NONE',  #95641 ) ;
#7986=EDGE_CURVE ( 'NONE', #28861, #45664, #8961, .T. ) ;
#7988=LINE ( 'NONE', #71875, #138952 ) ;
#7989=EDGE_LOOP ( 'NONE', ( #36420, #10079, #129452, #12956 ) ) ;
#7990=ADVANCED_FACE ( 'NONE', ( #106891 ), #9717, .F. ) ;
#7991=ORIENTED_EDGE ( 'NONE', *, *, #51924, .F. ) ;
#7992=LINE ( 'NONE', #18137, #9913 ) ;
#7993=LINE ( 'NONE', #18887, #64555 ) ;
#7995=DIRECTION ( 'NONE',  ( 0.7071067811865487940, 0.7071067811865463515, 0.000000000000000000 ) ) ;
#7996=CARTESIAN_POINT ( 'NONE',  ( -6.328169399223481761, -3.740707523384243505, 4.000000000000000000 ) ) ;
#7998=LINE ( 'NONE', #32649, #76246 ) ;
#7999=EDGE_CURVE ( 'NONE', #48100, #79180, #43796, .T. ) ;
#8000=DIRECTION ( 'NONE',  ( 0.6830127018922180770, -0.6830127018922204085, -0.2588190451025213501 ) ) ;
#8001=VECTOR ( 'NONE', #21950, 1000.000000000000000 ) ;
#8002=CARTESIAN_POINT ( 'NONE',  ( 34.92499999999998295, 16.80009451602700210, 4.759050581649325373 ) ) ;
#8003=DIRECTION ( 'NONE',  ( -0.6830127018922181881, 0.6830127018922202975, -0.2588190451025214056 ) ) ;
#8004=DIRECTION ( 'NONE',  ( 0.7071067811865486830, -0.7071067811865464625, -0.000000000000000000 ) ) ;
#8005=CARTESIAN_POINT ( 'NONE',  ( -5.816011393731002066, 28.73617430169783304, 5.000000000000000000 ) ) ;
#8006=DIRECTION ( 'NONE',  ( 0.3543493200069162685, -0.000000000000000000, -0.9351131265310288487 ) ) ;
#8007=LINE ( 'NONE', #29074, #76845 ) ;
#8008=CARTESIAN_POINT ( 'NONE',  ( -33.18398860626899705, 28.73617430169810305, 5.000000000000000000 ) ) ;
#8009=ADVANCED_FACE ( 'NONE', ( #129358 ), #42393, .F. ) ;
#8010=LINE ( 'NONE', #74014, #21091 ) ;
#8012=EDGE_LOOP ( 'NONE', ( #71243, #72278, #123249, #135978 ) ) ;
#8014=VERTEX_POINT ( 'NONE', #8268 ) ;
#8016=ORIENTED_EDGE ( 'NONE', *, *, #37641, .F. ) ;
#8018=ORIENTED_EDGE ( 'NONE', *, *, #83115, .T. ) ;
#8019=DIRECTION ( 'NONE',  ( 0.7071067811865487940, 0.7071067811865463515, 0.000000000000000000 ) ) ;
#8020=FACE_OUTER_BOUND ( 'NONE', #86538, .T. ) ;
#8021=ORIENTED_EDGE ( 'NONE', *, *, #19804, .T. ) ;
#8023=DIRECTION ( 'NONE',  ( 0.7071067811865487940, 0.7071067811865463515, 0.000000000000000000 ) ) ;
#8024=CARTESIAN_POINT ( 'NONE',  ( -33.12147316337127023, -20.24070752338407075, 7.412974875817869069 ) ) ;
#8025=DIRECTION ( 'NONE',  ( -0.000000000000000000, -0.3543493200069152693, 0.9351131265310292928 ) ) ;
#8027=ORIENTED_EDGE ( 'NONE', *, *, #87812, .F. ) ;
#8030=DIRECTION ( 'NONE',  ( 0.3543493200069162685, -0.000000000000000000, -0.9351131265310288487 ) ) ;
#8031=FACE_OUTER_BOUND ( 'NONE', #103682, .T. ) ;
#8033=CARTESIAN_POINT ( 'NONE',  ( -17.81601139373099940, 28.73617430169775133, 5.000000000000000000 ) ) ;
#8034=FACE_OUTER_BOUND ( 'NONE', #29804, .T. ) ;
#8036=VECTOR ( 'NONE', #14825, 1000.000000000000114 ) ;
#8037=CARTESIAN_POINT ( 'NONE',  ( 16.49999999999988987, 21.05218569542895679, 5.000000000000000000 ) ) ;
#8038=EDGE_CURVE ( 'NONE', #69227, #121031, #64841, .T. ) ;
#8039=VECTOR ( 'NONE', #3676, 1000.000000000000000 ) ;
#8040=ORIENTED_EDGE ( 'NONE', *, *, #39045, .F. ) ;
#8042=VECTOR ( 'NONE', #112322, 1000.000000000000000 ) ;
#8044=EDGE_LOOP ( 'NONE', ( #69150, #85237, #100776 ) ) ;
#8046=DIRECTION ( 'NONE',  ( -0.7071067811865486830, 0.7071067811865464625, 0.000000000000000000 ) ) ;
#8049=CARTESIAN_POINT ( 'NONE',  ( -51.29974487139158867, -27.71228299555242103, 4.000000000000000000 ) ) ;
#8050=CARTESIAN_POINT ( 'NONE',  ( 24.79289321881328689, -17.24070752338409918, 5.000000000000000000 ) ) ;
#8053=VERTEX_POINT ( 'NONE', #87302 ) ;
#8054=LINE ( 'NONE', #571, #85045 ) ;
#8055=ORIENTED_EDGE ( 'NONE', *, *, #101657, .F. ) ;
#8056=LINE ( 'NONE', #126991, #130699 ) ;
#8057=PLANE ( 'NONE',  #15366 ) ;
#8059=CARTESIAN_POINT ( 'NONE',  ( -19.78678096696629041, 12.75929247661559351, 10.29404684609030696 ) ) ;
#8060=ORIENTED_EDGE ( 'NONE', *, *, #130943, .F. ) ;
#8062=EDGE_LOOP ( 'NONE', ( #111725, #14219, #27039, #77689 ) ) ;
#8063=DIRECTION ( 'NONE',  ( 1.000000000000000000, 0.000000000000000000, 0.000000000000000000 ) ) ;
#8064=CARTESIAN_POINT ( 'NONE',  ( -24.18398860626899705, 28.73617430169804265, 5.000000000000000000 ) ) ;
#8066=LINE ( 'NONE', #41428, #2080 ) ;
#8068=ORIENTED_EDGE ( 'NONE', *, *, #44662, .T. ) ;
#8069=DIRECTION ( 'NONE',  ( 0.7071067811865486830, -0.7071067811865464625, -0.000000000000000000 ) ) ;
#8070=ORIENTED_EDGE ( 'NONE', *, *, #107199, .T. ) ;
#8071=EDGE_CURVE ( 'NONE', #56522, #75711, #25585, .T. ) ;
#8073=ORIENTED_EDGE ( 'NONE', *, *, #84301, .T. ) ;
#8074=DIRECTION ( 'NONE',  ( 1.000000000000000000, 0.000000000000000000, 0.000000000000000000 ) ) ;
#8076=ORIENTED_EDGE ( 'NONE', *, *, #139424, .F. ) ;
#8078=CARTESIAN_POINT ( 'NONE',  ( -1.499999999999987566, 6.052185695429108669, 5.000000000000000000 ) ) ;
#8079=CARTESIAN_POINT ( 'NONE',  ( 21.29974487139158512, -27.71228299555221142, 4.000000000000000000 ) ) ;
#8081=FACE_BOUND ( 'NONE', #41959, .T. ) ;
#8082=ORIENTED_EDGE ( 'NONE', *, *, #110078, .T. ) ;
#8083=LINE ( 'NONE', #141490, #133659 ) ;
#8084=EDGE_CURVE ( 'NONE', #95696, #109538, #111918, .T. ) ;
#8085=EDGE_CURVE ( 'NONE', #64063, #69181, #89431, .T. ) ;
#8086=CARTESIAN_POINT ( 'NONE',  ( 12.00548008471251293, 28.92564299267929684, 4.000000000000000000 ) ) ;
#8087=LINE ( 'NONE', #52328, #108698 ) ;
#8088=VERTEX_POINT ( 'NONE', #13991 ) ;
#8090=EDGE_LOOP ( 'NONE', ( #47374, #124652, #3641, #110715 ) ) ;
#8091=VERTEX_POINT ( 'NONE', #55399 ) ;
#8092=CARTESIAN_POINT ( 'NONE',  ( -3.183988606268992161, 28.73617430169789699, 5.000000000000000000 ) ) ;
#8093=ORIENTED_EDGE ( 'NONE', *, *, #31216, .T. ) ;
#8094=ADVANCED_FACE ( 'NONE', ( #11121 ), #47416, .F. ) ;
#8095=EDGE_CURVE ( 'NONE', #79128, #68609, #57548, .T. ) ;
#8097=ORIENTED_EDGE ( 'NONE', *, *, #41856, .F. ) ;
#8098=CARTESIAN_POINT ( 'NONE',  ( -19.22850677138653452, 20.25929247661551713, 7.808871592221724001 ) ) ;
#8099=AXIS2_PLACEMENT_3D ( 'NONE', #24109, #75993, #120164 ) ;
#8100=DIRECTION ( 'NONE',  ( -0.3543493200069162685, -0.000000000000000000, -0.9351131265310288487 ) ) ;
#8101=EDGE_CURVE ( 'NONE', #112793, #52592, #250, .T. ) ;
#8103=FACE_OUTER_BOUND ( 'NONE', #39898, .T. ) ;
#8104=EDGE_CURVE ( 'NONE', #50012, #99801, #90143, .T. ) ;
#8105=CARTESIAN_POINT ( 'NONE',  ( 11.81601139373100651, 28.73617430169779041, 5.000000000000000000 ) ) ;
#8107=CARTESIAN_POINT ( 'NONE',  ( 34.42499999999998295, -15.02281430457044742, 5.000000000000000000 ) ) ;
#8108=LINE ( 'NONE', #140772, #94438 ) ;
#8110=PLANE ( 'NONE',  #44052 ) ;
#8112=EDGE_CURVE ( 'NONE', #127403, #49277, #46709, .T. ) ;
#8113=EDGE_LOOP ( 'NONE', ( #2525, #96399, #92241, #112138 ) ) ;
#8114=CARTESIAN_POINT ( 'NONE',  ( 37.78501580275787575, -3.740707523384248390, 15.76143240460133121 ) ) ;
#8115=CARTESIAN_POINT ( 'NONE',  ( 62.99451991528749772, 28.92564299267982264, 4.000000000000000000 ) ) ;
#8116=ORIENTED_EDGE ( 'NONE', *, *, #24005, .T. ) ;
#8117=ORIENTED_EDGE ( 'NONE', *, *, #25842, .F. ) ;
#8118=ORIENTED_EDGE ( 'NONE', *, *, #124383, .F. ) ;
#8119=CARTESIAN_POINT ( 'NONE',  ( -26.99451991528749417, 28.92564299267956685, 4.000000000000000000 ) ) ;
#8120=DIRECTION ( 'NONE',  ( 0.7071067811865487940, 0.7071067811865463515, 0.000000000000000000 ) ) ;
#8121=LINE ( 'NONE', #75564, #25388 ) ;
#8122=ORIENTED_EDGE ( 'NONE', *, *, #127489, .T. ) ;
#8123=DIRECTION ( 'NONE',  ( 0.7071067811865486830, -0.7071067811865464625, -0.000000000000000000 ) ) ;
#8124=EDGE_CURVE ( 'NONE', #33017, #117585, #112618, .T. ) ;
#8125=DIRECTION ( 'NONE',  ( 0.7071067811865487940, -0.7071067811865463515, 0.000000000000000000 ) ) ;
#8126=VECTOR ( 'NONE', #126366, 999.9999999999998863 ) ;
#8128=AXIS2_PLACEMENT_3D ( 'NONE', #97653, #74507, #1861 ) ;
#8129=DIRECTION ( 'NONE',  ( -0.000000000000000000, 0.000000000000000000, 1.000000000000000000 ) ) ;
#8130=EDGE_LOOP ( 'NONE', ( #50108, #56244, #12565, #5862 ) ) ;
#8132=VECTOR ( 'NONE', #22366, 1000.000000000000000 ) ;
#8135=EDGE_CURVE ( 'NONE', #42962, #37411, #132977, .T. ) ;
#8136=CARTESIAN_POINT ( 'NONE',  ( -8.671830600776409881, 5.259292476615659240, 4.000000000000000000 ) ) ;
#8137=CARTESIAN_POINT ( 'NONE',  ( 5.994519915287488843, 28.92564299267942118, 4.000000000000000000 ) ) ;
#8138=ORIENTED_EDGE ( 'NONE', *, *, #12810, .T. ) ;
#8139=CARTESIAN_POINT ( 'NONE',  ( 0.000000000000000000, 0.000000000000000000, 5.000000000000000000 ) ) ;
#8140=VERTEX_POINT ( 'NONE', #56138 ) ;
#8142=PLANE ( 'NONE',  #63210 ) ;
#8145=EDGE_CURVE ( 'NONE', #116931, #52182, #2389, .T. ) ;
#8146=EDGE_CURVE ( 'NONE', #16679, #143518, #122042, .T. ) ;
#8147=DIRECTION ( 'NONE',  ( 0.7071067811865486830, -0.7071067811865464625, -0.000000000000000000 ) ) ;
#8148=CARTESIAN_POINT ( 'NONE',  ( -18.18398860626898994, 28.73617430169800002, 5.000000000000000000 ) ) ;
#8150=ORIENTED_EDGE ( 'NONE', *, *, #45348, .F. ) ;
#8151=DIRECTION ( 'NONE',  ( 0.7071067811865487940, 0.7071067811865463515, 0.000000000000000000 ) ) ;
#8152=FACE_OUTER_BOUND ( 'NONE', #19129, .T. ) ;
#8153=ADVANCED_FACE ( 'NONE', ( #80034 ), #66982, .F. ) ;
#8155=PLANE ( 'NONE',  #143331 ) ;
#8156=ORIENTED_EDGE ( 'NONE', *, *, #10276, .T. ) ;
#8157=VERTEX_POINT ( 'NONE', #45261 ) ;
#8160=ADVANCED_FACE ( 'NONE', ( #133665 ), #34346, .F. ) ;
#8165=ORIENTED_EDGE ( 'NONE', *, *, #101928, .T. ) ;
#8166=EDGE_CURVE ( 'NONE', #5483, #97574, #128328, .T. ) ;
#8167=DIRECTION ( 'NONE',  ( 0.7071067811865487940, 0.7071067811865463515, -0.000000000000000000 ) ) ;
#8168=FACE_OUTER_BOUND ( 'NONE', #72873, .T. ) ;
#8169=DIRECTION ( 'NONE',  ( -0.000000000000000000, -0.3543493200069152693, 0.9351131265310292928 ) ) ;
#8170=PLANE ( 'NONE',  #133933 ) ;
#8172=DIRECTION ( 'NONE',  ( -0.000000000000000000, -0.000000000000000000, 1.000000000000000000 ) ) ;
#8173=VERTEX_POINT ( 'NONE', #14731 ) ;
#8175=ORIENTED_EDGE ( 'NONE', *, *, #42029, .T. ) ;
#8176=ORIENTED_EDGE ( 'NONE', *, *, #130934, .T. ) ;
#8177=DIRECTION ( 'NONE',  ( 0.000000000000000000, -1.000000000000000000, 0.000000000000000000 ) ) ;
#8178=LINE ( 'NONE', #41536, #60224 ) ;
#8179=EDGE_LOOP ( 'NONE', ( #80359, #130720, #28171, #780 ) ) ;
#8181=LINE ( 'NONE', #143012, #51189 ) ;
#8182=CARTESIAN_POINT ( 'NONE',  ( 69.18398860626899705, 28.73617430169835529, 5.000000000000000000 ) ) ;
#8183=EDGE_CURVE ( 'NONE', #88988, #47967, #59007, .T. ) ;
#8185=CARTESIAN_POINT ( 'NONE',  ( -45.48921356237309510, -27.52281430457087197, 5.000000000000000000 ) ) ;
#8186=EDGE_LOOP ( 'NONE', ( #87949, #100295, #96738, #7739 ) ) ;
#8187=CARTESIAN_POINT ( 'NONE',  ( -27.48921356237309155, -27.52281430457074762, 5.000000000000000000 ) ) ;
#8188=DIRECTION ( 'NONE',  ( -0.3543493200069162685, -0.000000000000000000, -0.9351131265310288487 ) ) ;
#8189=CARTESIAN_POINT ( 'NONE',  ( -33.79289321881321939, -5.240707523384230626, 5.000000000000000000 ) ) ;
#8190=CARTESIAN_POINT ( 'NONE',  ( -29.99451991528749417, 28.92564299267958816, 4.000000000000000000 ) ) ;
#8191=DIRECTION ( 'NONE',  ( -0.7071067811865486830, 0.7071067811865464625, 0.000000000000000000 ) ) ;
#8193=VECTOR ( 'NONE', #121460, 1000.000000000000227 ) ;
#8194=ADVANCED_FACE ( 'NONE', ( #103163 ), #7934, .F. ) ;
#8196=VERTEX_POINT ( 'NONE', #25590 ) ;
#8199=CARTESIAN_POINT ( 'NONE',  ( -18.54365462162017408, -22.22500000000000142, 11.20750413071516860 ) ) ;
#8200=VECTOR ( 'NONE', #66408, 1000.000000000000227 ) ;
#8201=DIRECTION ( 'NONE',  ( 0.3543493200069162685, -0.000000000000000000, -0.9351131265310288487 ) ) ;
#8202=PLANE ( 'NONE',  #15869 ) ;
#8203=ORIENTED_EDGE ( 'NONE', *, *, #12379, .T. ) ;
#8204=EDGE_CURVE ( 'NONE', #32743, #47525, #6473, .T. ) ;
#8205=CARTESIAN_POINT ( 'NONE',  ( -24.79289321881328334, -5.240707523384232402, 5.000000000000000000 ) ) ;
#8209=EDGE_LOOP ( 'NONE', ( #129631, #49857, #123730, #64388 ) ) ;
#8210=CARTESIAN_POINT ( 'NONE',  ( 7.176659101599685009, 5.259292476615659240, 15.86257073897096070 ) ) ;
#8211=ORIENTED_EDGE ( 'NONE', *, *, #65018, .T. ) ;
#8212=ORIENTED_EDGE ( 'NONE', *, *, #87043, .T. ) ;
#8213=CARTESIAN_POINT ( 'NONE',  ( -42.48921356237308800, -27.52281430457085065, 5.000000000000000000 ) ) ;
#8214=CARTESIAN_POINT ( 'NONE',  ( 13.49999999999990763, 13.56627193232216477, -10.57019076586065687 ) ) ;
#8215=DIRECTION ( 'NONE',  ( -0.6830127018922181881, 0.6830127018922202975, -0.2588190451025214056 ) ) ;
#8216=ORIENTED_EDGE ( 'NONE', *, *, #78718, .T. ) ;
#8217=EDGE_CURVE ( 'NONE', #43879, #60787, #40602, .T. ) ;
#8218=CARTESIAN_POINT ( 'NONE',  ( -34.49999999999976552, 3.073033219394595505, -6.593910359671048660 ) ) ;
#8219=LINE ( 'NONE', #82273, #142461 ) ;
#8220=EDGE_LOOP ( 'NONE', ( #127151, #108096, #64112, #93756 ) ) ;
#8221=CARTESIAN_POINT ( 'NONE',  ( 23.60898926630779826, -0.6778661889157658882, 4.000000000000000000 ) ) ;
#8222=DIRECTION ( 'NONE',  ( -0.7071067811865486830, -0.7071067811865464625, 0.000000000000000000 ) ) ;
#8223=DIRECTION ( 'NONE',  ( -0.6830127018922180770, -0.6830127018922204085, -0.2588190451025213501 ) ) ;
#8224=FACE_OUTER_BOUND ( 'NONE', #31463, .T. ) ;
#8225=VECTOR ( 'NONE', #5552, 1000.000000000000000 ) ;
#8226=EDGE_LOOP ( 'NONE', ( #43644, #77141, #125012, #42026 ) ) ;
#8227=VECTOR ( 'NONE', #104321, 1000.000000000000000 ) ;
#8228=VERTEX_POINT ( 'NONE', #97056 ) ;
#8230=CARTESIAN_POINT ( 'NONE',  ( -17.99999999999986855, 20.96639925780204905, 5.000000000000000000 ) ) ;
#8233=DIRECTION ( 'NONE',  ( -0.7071067811865486830, -0.7071067811865464625, -0.000000000000000000 ) ) ;
#8234=CARTESIAN_POINT ( 'NONE',  ( 25.49999999999982592, 6.277155672890295079, -3.510561720659000962 ) ) ;
#8235=ORIENTED_EDGE ( 'NONE', *, *, #33880, .T. ) ;
#8237=VECTOR ( 'NONE', #41908, 1000.000000000000000 ) ;
#8238=DIRECTION ( 'NONE',  ( -0.000000000000000000, -0.3543493200069152693, 0.9351131265310292928 ) ) ;
#8239=PLANE ( 'NONE',  #23645 ) ;
#8240=VERTEX_POINT ( 'NONE', #39167 ) ;
#8241=EDGE_LOOP ( 'NONE', ( #128185, #116395, #126319, #96183 ) ) ;
#8242=PLANE ( 'NONE',  #120828 ) ;
#8243=ORIENTED_EDGE ( 'NONE', *, *, #66429, .F. ) ;
#8245=EDGE_CURVE ( 'NONE', #134120, #99796, #139926, .T. ) ;
#8246=DIRECTION ( 'NONE',  ( -0.7071067811865486830, -0.7071067811865464625, -0.000000000000000000 ) ) ;
#8247=PLANE ( 'NONE',  #9467 ) ;
#8248=FACE_BOUND ( 'NONE', #131821, .T. ) ;
#8249=CARTESIAN_POINT ( 'NONE',  ( -7.499999999999947597, -16.91253812416058011, 4.000000000000000000 ) ) ;
#8250=EDGE_CURVE ( 'NONE', #63037, #14142, #29002, .T. ) ;
#8252=FACE_OUTER_BOUND ( 'NONE', #92686, .T. ) ;
#8253=CARTESIAN_POINT ( 'NONE',  ( 54.29974487139159578, -27.71228299555243879, 4.000000000000000000 ) ) ;
#8254=EDGE_LOOP ( 'NONE', ( #67768, #138531, #123832 ) ) ;
#8255=CARTESIAN_POINT ( 'NONE',  ( 20.99999999999985079, 12.83542986846998879, -1.025386466790417561 ) ) ;
#8258=EDGE_CURVE ( 'NONE', #88739, #75266, #116720, .T. ) ;
#8261=ORIENTED_EDGE ( 'NONE', *, *, #61575, .F. ) ;
#8262=DIRECTION ( 'NONE',  ( 0.7071067811865487940, -0.7071067811865463515, 0.000000000000000000 ) ) ;
#8263=ADVANCED_FACE ( 'NONE', ( #29689 ), #94943, .F. ) ;
#8264=DIRECTION ( 'NONE',  ( 0.6830127018922180770, -0.6830127018922204085, -0.2588190451025213501 ) ) ;
#8265=EDGE_CURVE ( 'NONE', #100067, #19260, #18073, .T. ) ;
#8266=CARTESIAN_POINT ( 'NONE',  ( 5.700255128608413102, -27.71228299555201957, 4.000000000000000000 ) ) ;
#8267=ADVANCED_FACE ( 'NONE', ( #106520 ), #7204, .F. ) ;
#8268=CARTESIAN_POINT ( 'NONE',  ( -27.79289321881325847, 6.759292476615649470, 5.000000000000000000 ) ) ;
#8269=CARTESIAN_POINT ( 'NONE',  ( 66.48921356237309510, -27.52281430457101763, 5.000000000000000000 ) ) ;
#8270=EDGE_CURVE ( 'NONE', #91367, #116472, #51476, .T. ) ;
#8271=CARTESIAN_POINT ( 'NONE',  ( 30.29974487139158867, -27.71228299555227537, 4.000000000000000000 ) ) ;
#8272=DIRECTION ( 'NONE',  ( -0.7071067811865486830, -0.7071067811865464625, -0.000000000000000000 ) ) ;
#8273=PLANE ( 'NONE',  #61222 ) ;
#8275=FACE_OUTER_BOUND ( 'NONE', #8226, .T. ) ;
#8276=ORIENTED_EDGE ( 'NONE', *, *, #74717, .F. ) ;
#8278=VERTEX_POINT ( 'NONE', #30431 ) ;
#8279=CARTESIAN_POINT ( 'NONE',  ( -26.99451991528749417, 28.92564299267956685, 4.000000000000000000 ) ) ;
#8281=EDGE_CURVE ( 'NONE', #20176, #46795, #74665, .T. ) ;
#8282=ORIENTED_EDGE ( 'NONE', *, *, #117272, .T. ) ;
#8283=EDGE_LOOP ( 'NONE', ( #52578, #8176, #30633, #98962 ) ) ;
#8284=ORIENTED_EDGE ( 'NONE', *, *, #32742, .F. ) ;
#8286=ORIENTED_EDGE ( 'NONE', *, *, #141206, .F. ) ;
#8289=AXIS2_PLACEMENT_3D ( 'NONE', #118642, #65745, #20750 ) ;
#8292=ORIENTED_EDGE ( 'NONE', *, *, #3439, .T. ) ;
#8293=AXIS2_PLACEMENT_3D ( 'NONE', #38413, #49316, #93503 ) ;
#8294=LINE ( 'NONE', #95332, #115140 ) ;
#8296=DIRECTION ( 'NONE',  ( 0.6830127018922181881, 0.6830127018922202975, -0.2588190451025214056 ) ) ;
#8297=DIRECTION ( 'NONE',  ( -0.3543493200069162685, -0.000000000000000000, -0.9351131265310288487 ) ) ;
#8298=DIRECTION ( 'NONE',  ( -0.7071067811865486830, 0.7071067811865464625, 0.000000000000000000 ) ) ;
#8299=ORIENTED_EDGE ( 'NONE', *, *, #73425, .T. ) ;
#8300=ORIENTED_EDGE ( 'NONE', *, *, #106751, .T. ) ;
#8301=DIRECTION ( 'NONE',  ( -0.6830127018922181881, 0.6830127018922202975, -0.2588190451025214056 ) ) ;
#8302=DIRECTION ( 'NONE',  ( -0.7071067811865487940, 0.7071067811865463515, 0.000000000000000000 ) ) ;
#8303=EDGE_LOOP ( 'NONE', ( #51416, #41280, #113016 ) ) ;
#8305=EDGE_LOOP ( 'NONE', ( #44939, #106234, #43319, #43706 ) ) ;
#8306=ORIENTED_EDGE ( 'NONE', *, *, #118474, .F. ) ;
#8307=ORIENTED_EDGE ( 'NONE', *, *, #117298, .T. ) ;
#8308=VECTOR ( 'NONE', #8354, 1000.000000000000000 ) ;
#8309=EDGE_CURVE ( 'NONE', #23928, #16647, #44172, .T. ) ;
#8310=LINE ( 'NONE', #120654, #24022 ) ;
#8311=DIRECTION ( 'NONE',  ( -0.7071067811865486830, 0.7071067811865464625, 0.000000000000000000 ) ) ;
#8312=EDGE_CURVE ( 'NONE', #113821, #56274, #34007, .T. ) ;
#8313=CARTESIAN_POINT ( 'NONE',  ( 34.45011844616453800, 0.002304141593939786677, 5.000000000000001776 ) ) ;
#8314=CARTESIAN_POINT ( 'NONE',  ( 62.99451991528749772, 28.92564299267982264, 4.000000000000000000 ) ) ;
#8315=DIRECTION ( 'NONE',  ( -0.6830127018922180770, -0.6830127018922204085, -0.2588190451025213501 ) ) ;
#8316=ORIENTED_EDGE ( 'NONE', *, *, #33135, .F. ) ;
#8317=PLANE ( 'NONE',  #297 ) ;
#8318=VERTEX_POINT ( 'NONE', #12224 ) ;
#8319=DIRECTION ( 'NONE',  ( 0.7071067811865486830, -0.7071067811865464625, -0.000000000000000000 ) ) ;
#8320=ADVANCED_FACE ( 'NONE', ( #56514 ), #21692, .F. ) ;
#8321=VECTOR ( 'NONE', #80676, 999.9999999999998863 ) ;
#8323=VECTOR ( 'NONE', #123475, 999.9999999999998863 ) ;
#8324=ORIENTED_EDGE ( 'NONE', *, *, #62035, .T. ) ;
#8325=DIRECTION ( 'NONE',  ( -0.000000000000000000, -0.3543493200069152693, 0.9351131265310292928 ) ) ;
#8326=CARTESIAN_POINT ( 'NONE',  ( 11.67183060077639212, -18.74070752338409207, 4.000000000000000000 ) ) ;
#8327=ORIENTED_EDGE ( 'NONE', *, *, #64477, .F. ) ;
#8330=CARTESIAN_POINT ( 'NONE',  ( 25.49999999999983302, 16.08746187583908238, 4.000000000000000000 ) ) ;
#8332=CARTESIAN_POINT ( 'NONE',  ( -3.489213562373097322, -27.52281430457057709, 5.000000000000000000 ) ) ;
#8333=AXIS2_PLACEMENT_3D ( 'NONE', #122128, #114638, #25485 ) ;
#8334=CARTESIAN_POINT ( 'NONE',  ( 34.17183060077621803, -2.240707523384275035, 4.000000000000000000 ) ) ;
#8335=FACE_OUTER_BOUND ( 'NONE', #97810, .T. ) ;
#8338=DIRECTION ( 'NONE',  ( 0.7071067811865487940, 0.7071067811865463515, 0.000000000000000000 ) ) ;
#8339=PLANE ( 'NONE',  #39553 ) ;
#8340=ADVANCED_FACE ( 'NONE', ( #44925 ), #77529, .F. ) ;
#8341=CARTESIAN_POINT ( 'NONE',  ( -29.99451991528749417, 28.92564299267958816, 4.000000000000000000 ) ) ;
#8343=CARTESIAN_POINT ( 'NONE',  ( -17.61782366839360847, 8.969638207445433054, 4.000000000000000000 ) ) ;
#8344=ORIENTED_EDGE ( 'NONE', *, *, #45209, .F. ) ;
#8345=DIRECTION ( 'NONE',  ( 1.000000000000000000, 0.000000000000000000, 0.000000000000000000 ) ) ;
#8346=FACE_OUTER_BOUND ( 'NONE', #58279, .T. ) ;
#8347=ORIENTED_EDGE ( 'NONE', *, *, #119887, .T. ) ;
#8348=CARTESIAN_POINT ( 'NONE',  ( 11.99999999999991651, -21.03360074219752462, 5.000000000000000000 ) ) ;
#8349=DIRECTION ( 'NONE',  ( 0.6830127018922180770, -0.6830127018922204085, -0.2588190451025213501 ) ) ;
#8350=VERTEX_POINT ( 'NONE', #109407 ) ;
#8351=FACE_OUTER_BOUND ( 'NONE', #45483, .T. ) ;
#8352=ADVANCED_FACE ( 'NONE', ( #108655 ), #120241, .T. ) ;
#8353=CARTESIAN_POINT ( 'NONE',  ( -12.18398860626900060, 28.73617430169795739, 5.000000000000000000 ) ) ;
#8354=DIRECTION ( 'NONE',  ( -0.7071067811865486830, -0.7071067811865464625, 0.000000000000000000 ) ) ;
#8355=ORIENTED_EDGE ( 'NONE', *, *, #75912, .T. ) ;
#8356=ORIENTED_EDGE ( 'NONE', *, *, #50718, .F. ) ;
#8357=DIRECTION ( 'NONE',  ( 0.7071067811865487940, -0.7071067811865463515, 0.000000000000000000 ) ) ;
#8360=CARTESIAN_POINT ( 'NONE',  ( 7.499999999999947597, -17.91344420646041513, 1.358650452708480838 ) ) ;
#8361=EDGE_CURVE ( 'NONE', #9887, #19214, #65946, .T. ) ;
#8362=CARTESIAN_POINT ( 'NONE',  ( -48.18398860626899705, 28.73617430169820608, 5.000000000000000000 ) ) ;
#8363=ORIENTED_EDGE ( 'NONE', *, *, #11562, .F. ) ;
#8364=CARTESIAN_POINT ( 'NONE',  ( 42.18398860626899705, 28.73617430169816700, 5.000000000000000000 ) ) ;
#8365=CARTESIAN_POINT ( 'NONE',  ( -36.18398860626899705, 28.73617430169812437, 5.000000000000000000 ) ) ;
#8367=VECTOR ( 'NONE', #80656, 1000.000000000000000 ) ;
#8368=ORIENTED_EDGE ( 'NONE', *, *, #54023, .T. ) ;
#8369=EDGE_CURVE ( 'NONE', #95585, #117852, #120989, .T. ) ;
#8370=LINE ( 'NONE', #52620, #7372 ) ;
#8372=EDGE_CURVE ( 'NONE', #66020, #30015, #9336, .T. ) ;
#8374=LINE ( 'NONE', #96812, #105649 ) ;
#8375=VECTOR ( 'NONE', #128567, 1000.000000000000000 ) ;
#8376=CYLINDRICAL_SURFACE ( 'NONE', #111927, 0.5000000000000004441 ) ;
#8377=ORIENTED_EDGE ( 'NONE', *, *, #86002, .F. ) ;
#8378=CARTESIAN_POINT ( 'NONE',  ( -6.938893903907228378E-15, -22.22500000000000142, 4.412002311790018894 ) ) ;
#8380=LINE ( 'NONE', #143222, #99507 ) ;
#8381=ADVANCED_FACE ( 'NONE', ( #20959 ), #32581, .F. ) ;
#8382=DIRECTION ( 'NONE',  ( 1.000000000000000000, 0.000000000000000000, 0.000000000000000000 ) ) ;
#8383=CARTESIAN_POINT ( 'NONE',  ( 8.671830600776408104, -18.74070752338409562, 4.000000000000000000 ) ) ;
#8384=EDGE_LOOP ( 'NONE', ( #62204, #81962, #115931, #2503 ) ) ;
#8386=DIRECTION ( 'NONE',  ( -0.7071067811865487940, 0.7071067811865463515, -0.000000000000000000 ) ) ;
#8387=CARTESIAN_POINT ( 'NONE',  ( 6.792893218813412126, -17.24070752338409918, 5.000000000000000000 ) ) ;
#8388=LINE ( 'NONE', #63566, #51635 ) ;
#8389=ORIENTED_EDGE ( 'NONE', *, *, #15356, .F. ) ;
#8391=EDGE_LOOP ( 'NONE', ( #102492, #58422, #60287, #71616, #12586 ) ) ;
#8393=ORIENTED_EDGE ( 'NONE', *, *, #52343, .F. ) ;
#8394=VECTOR ( 'NONE', #41085, 1000.000000000000000 ) ;
#8395=DIRECTION ( 'NONE',  ( 0.3543493200069162685, -0.000000000000000000, -0.9351131265310288487 ) ) ;
#8397=PLANE ( 'NONE',  #124477 ) ;
#8398=ORIENTED_EDGE ( 'NONE', *, *, #117361, .F. ) ;
#8399=CARTESIAN_POINT ( 'NONE',  ( -7.499999999999947597, 21.43112307739195899, 4.000000000000000000 ) ) ;
#8400=DIRECTION ( 'NONE',  ( 0.7071067811865487940, -0.7071067811865463515, 0.000000000000000000 ) ) ;
#8401=ORIENTED_EDGE ( 'NONE', *, *, #50698, .T. ) ;
#8404=CARTESIAN_POINT ( 'NONE',  ( -17.99999999999986855, -9.412538124160658271, 4.000000000000000000 ) ) ;
#8405=DIRECTION ( 'NONE',  ( 0.7071067811865486830, -0.7071067811865464625, -0.000000000000000000 ) ) ;
#8406=ORIENTED_EDGE ( 'NONE', *, *, #12714, .T. ) ;
#8409=FACE_BOUND ( 'NONE', #141749, .T. ) ;
#8410=DIRECTION ( 'NONE',  ( -0.7071067811865486830, 0.7071067811865464625, 0.000000000000000000 ) ) ;
#8413=VECTOR ( 'NONE', #142553, 1000.000000000000000 ) ;
#8416=ORIENTED_EDGE ( 'NONE', *, *, #35686, .F. ) ;
#8419=AXIS2_PLACEMENT_3D ( 'NONE', #94653, #48313, #38172 ) ;
#8420=ORIENTED_EDGE ( 'NONE', *, *, #88850, .T. ) ;
#8421=ORIENTED_EDGE ( 'NONE', *, *, #72908, .T. ) ;
#8422=EDGE_CURVE ( 'NONE', #56693, #69078, #65223, .T. ) ;
#8423=VERTEX_POINT ( 'NONE', #54356 ) ;
#8424=ADVANCED_FACE ( 'NONE', ( #11487 ), #110105, .F. ) ;
#8426=EDGE_CURVE ( 'NONE', #95580, #110421, #133326, .T. ) ;
#8427=PLANE ( 'NONE',  #80294 ) ;
#8428=DIRECTION ( 'NONE',  ( -0.6830127018922180770, -0.6830127018922204085, -0.2588190451025213501 ) ) ;
#8429=ORIENTED_EDGE ( 'NONE', *, *, #139279, .T. ) ;
#8430=CARTESIAN_POINT ( 'NONE',  ( 5.999999999999956479, 10.21212019023809425, -2.019456568337813618 ) ) ;
#8431=FACE_OUTER_BOUND ( 'NONE', #37648, .T. ) ;
#8432=CARTESIAN_POINT ( 'NONE',  ( 54.18398860626899705, 28.73617430169825226, 5.000000000000000000 ) ) ;
#8433=CARTESIAN_POINT ( 'NONE',  ( 19.82816939922339827, -11.24070752338416490, 4.000000000000000000 ) ) ;
#8435=ORIENTED_EDGE ( 'NONE', *, *, #54856, .T. ) ;
#8436=DIRECTION ( 'NONE',  ( 1.000000000000000000, 0.000000000000000000, 0.000000000000000000 ) ) ;
#8437=CARTESIAN_POINT ( 'NONE',  ( -34.92500000000001137, 22.22500000000000142, 4.500000000000000888 ) ) ;
#8438=ADVANCED_FACE ( 'NONE', ( #10779 ), #143455, .F. ) ;
#8439=EDGE_LOOP ( 'NONE', ( #116205, #40188, #80561, #1678, #48501, #54430, #75050, #32377, #85686, #67372, #12732, #117488, #77270, #45063, #78163, #45850, #56486, #59786, #34834, #87725, #18343, #45859, #85137, #78966, #90063, #129037, #104834, #25897, #120091, #99854, #49346, #34602, #89588, #93558, #25627, #136956, #135091, #19962, #101101, #128821, #55730, #14420, #103492, #133848, #91553, #108559, #79515, #49077, #17830, #81463, #45027, #100112, #132014, #115819, #67460, #70467, #79197, #89364, #93014, #96089, #88001, #69804, #116746, #3975, #131956, #56600, #65930, #137007, #92932, #39828, #111856, #114689, #92312, #65058, #95664, #82493, #80044, #73536, #29085, #124784, #82603, #124503, #109596, #85096, #31050, #96321, #13328, #11755, #55763, #132687, #19155, #51883, #47116, #83134, #61645, #84972, #94015, #17633, #100447, #104628, #88695, #15426, #21846, #88106, #39479, #30980, #8564, #19916, #92589, #15684, #140590, #129596, #130954, #40036, #69127, #84861, #51632, #2218, #64516, #73874, #39572, #50448, #55420, #23522, #141251, #110761, #87642, #20053, #18326, #76101, #104419, #9856, #53450, #11339, #136908, #22862, #62081, #80292, #654, #80061, #118677, #60620, #134783, #3446, #103285, #127752, #3790, #16988, #90342, #7947, #132801, #93874, #115537, #73124, #79819, #140944, #105162, #110819, #119872, #31043, #10860, #85177, #109564, #140235, #87789 ) ) ;
#8440=CARTESIAN_POINT ( 'NONE',  ( -34.92500000000001137, 20.71849043720401795, 4.759050581649336920 ) ) ;
#8441=ORIENTED_EDGE ( 'NONE', *, *, #73373, .T. ) ;
#8442=VERTEX_POINT ( 'NONE', #630 ) ;
#8443=EDGE_CURVE ( 'NONE', #104684, #49293, #23077, .T. ) ;
#8444=ORIENTED_EDGE ( 'NONE', *, *, #142641, .T. ) ;
#8446=ORIENTED_EDGE ( 'NONE', *, *, #122013, .F. ) ;
#8447=EDGE_LOOP ( 'NONE', ( #17832, #98399, #47790, #23353 ) ) ;
#8448=EDGE_CURVE ( 'NONE', #57879, #93602, #25977, .T. ) ;
#8449=LINE ( 'NONE', #52702, #113707 ) ;
#8450=VECTOR ( 'NONE', #116568, 1000.000000000000227 ) ;
#8451=DIRECTION ( 'NONE',  ( -0.6830127018922180770, -0.6830127018922204085, -0.2588190451025213501 ) ) ;
#8453=LINE ( 'NONE', #20793, #77571 ) ;
#8454=FACE_OUTER_BOUND ( 'NONE', #27915, .T. ) ;
#8455=VERTEX_POINT ( 'NONE', #68792 ) ;
#8457=EDGE_CURVE ( 'NONE', #60173, #89845, #1336, .T. ) ;
#8458=VECTOR ( 'NONE', #2893, 1000.000000000000114 ) ;
#8460=( BOUNDED_CURVE ( )  B_SPLINE_CURVE ( 3, ( #127243, #75053, #51139, #27946 ),
 .UNSPECIFIED., .F., .F. ) 
 B_SPLINE_CURVE_WITH_KNOTS ( ( 4, 4 ),
 ( 1.864375635226928729, 1.933014472006540752 ),
 .UNSPECIFIED. ) 
 CURVE ( )  GEOMETRIC_REPRESENTATION_ITEM ( )  RATIONAL_B_SPLINE_CURVE ( ( 1.000000000000000000, 0.9996074310407765395, 0.9996074310407765395, 1.000000000000000000 ) ) 
 REPRESENTATION_ITEM ( '' )  );
#8461=DIRECTION ( 'NONE',  ( 0.7071067811865487940, 0.7071067811865463515, -0.000000000000000000 ) ) ;
#8462=ORIENTED_EDGE ( 'NONE', *, *, #124054, .F. ) ;
#8463=DIRECTION ( 'NONE',  ( 0.6830127018922181881, 0.6830127018922202975, -0.2588190451025214056 ) ) ;
#8464=EDGE_LOOP ( 'NONE', ( #134851, #124825, #8327 ) ) ;
#8465=ORIENTED_EDGE ( 'NONE', *, *, #41221, .F. ) ;
#8467=EDGE_CURVE ( 'NONE', #139864, #78508, #69502, .T. ) ;
#8469=AXIS2_PLACEMENT_3D ( 'NONE', #93796, #27822, #72088 ) ;
#8470=VERTEX_POINT ( 'NONE', #3475 ) ;
#8471=( BOUNDED_CURVE ( )  B_SPLINE_CURVE ( 3, ( #98040, #121197, #10983, #130687 ),
 .UNSPECIFIED., .F., .T. ) 
 B_SPLINE_CURVE_WITH_KNOTS ( ( 4, 4 ),
 ( 2.001653308786168317, 3.503810798801451742 ),
 .UNSPECIFIED. ) 
 CURVE ( )  GEOMETRIC_REPRESENTATION_ITEM ( )  RATIONAL_B_SPLINE_CURVE ( ( 1.000000000000000000, 0.8206354192515236123, 0.8206354192515236123, 1.000000000000000000 ) ) 
 REPRESENTATION_ITEM ( '' )  );
#8472=CARTESIAN_POINT ( 'NONE',  ( 57.29974487139158157, -27.71228299555246011, 4.000000000000000000 ) ) ;
#8473=DIRECTION ( 'NONE',  ( 0.6830127018922180770, -0.6830127018922204085, -0.2588190451025213501 ) ) ;
#8474=VECTOR ( 'NONE', #135778, 1000.000000000000000 ) ;
#8475=CARTESIAN_POINT ( 'NONE',  ( -9.489213562373095101, -27.52281430457062328, 5.000000000000000000 ) ) ;
#8476=EDGE_LOOP ( 'NONE', ( #137256, #115609, #113109, #142312 ) ) ;
#8478=VERTEX_POINT ( 'NONE', #12932 ) ;
#8482=AXIS2_PLACEMENT_3D ( 'NONE', #10408, #64826, #52497 ) ;
#8485=EDGE_LOOP ( 'NONE', ( #112428, #92301, #140328, #102609 ) ) ;
#8486=EDGE_CURVE ( 'NONE', #745, #130461, #58664, .T. ) ;
#8487=VECTOR ( 'NONE', #66194, 999.9999999999998863 ) ;
#8488=ORIENTED_EDGE ( 'NONE', *, *, #98197, .F. ) ;
#8489=DIRECTION ( 'NONE',  ( -0.000000000000000000, 0.3543493200069153248, 0.9351131265310292928 ) ) ;
#8490=DIRECTION ( 'NONE',  ( -0.7071067811865486830, -0.7071067811865464625, 0.000000000000000000 ) ) ;
#8491=CARTESIAN_POINT ( 'NONE',  ( -8.510786437626906675, -27.52281430457049183, 5.000000000000000000 ) ) ;
#8493=CARTESIAN_POINT ( 'NONE',  ( 0.000000000000000000, 0.000000000000000000, 5.000000000000000000 ) ) ;
#8494=DIRECTION ( 'NONE',  ( -0.7071067811865486830, -0.7071067811865464625, 0.000000000000000000 ) ) ;
#8496=ADVANCED_FACE ( 'NONE', ( #68100 ), #79697, .F. ) ;
#8497=FACE_OUTER_BOUND ( 'NONE', #1428, .T. ) ;
#8498=DIRECTION ( 'NONE',  ( -0.7071067811865487940, 0.7071067811865463515, 0.000000000000000000 ) ) ;
#8499=ORIENTED_EDGE ( 'NONE', *, *, #7937, .F. ) ;
#8500=DIRECTION ( 'NONE',  ( 0.7071067811865486830, -0.7071067811865464625, -0.000000000000000000 ) ) ;
#8501=CARTESIAN_POINT ( 'NONE',  ( -24.29974487139158867, -27.71228299555223273, 4.000000000000000000 ) ) ;
#8502=VERTEX_POINT ( 'NONE', #36150 ) ;
#8503=CARTESIAN_POINT ( 'NONE',  ( 34.00193056682073944, -22.22500000000000142, 4.500000000000000888 ) ) ;
#8505=ORIENTED_EDGE ( 'NONE', *, *, #93613, .T. ) ;
#8506=EDGE_CURVE ( 'NONE', #21745, #29986, #48437, .T. ) ;
#8507=DIRECTION ( 'NONE',  ( 0.7071067811865486830, -0.7071067811865464625, -0.000000000000000000 ) ) ;
#8508=ORIENTED_EDGE ( 'NONE', *, *, #108832, .F. ) ;
#8509=DIRECTION ( 'NONE',  ( -0.7071067811865487940, 0.7071067811865463515, -0.000000000000000000 ) ) ;
#8510=ORIENTED_EDGE ( 'NONE', *, *, #121695, .T. ) ;
#8511=CARTESIAN_POINT ( 'NONE',  ( -19.30725242247703122, 9.139235811853158253, 4.261625515810906428 ) ) ;
#8512=ORIENTED_EDGE ( 'NONE', *, *, #137782, .T. ) ;
#8514=VECTOR ( 'NONE', #19681, 1000.000000000000000 ) ;
#8515=VECTOR ( 'NONE', #142675, 1000.000000000000000 ) ;
#8521=AXIS2_PLACEMENT_3D ( 'NONE', #35391, #99894, #44854 ) ;
#8524=VECTOR ( 'NONE', #111857, 1000.000000000000227 ) ;
#8525=CARTESIAN_POINT ( 'NONE',  ( -33.48921356237309510, -27.52281430457078670, 5.000000000000000000 ) ) ;
#8526=CARTESIAN_POINT ( 'NONE',  ( 34.47516574401890921, 15.02806734111565490, 4.998110765256834398 ) ) ;
#8527=ORIENTED_EDGE ( 'NONE', *, *, #137713, .T. ) ;
#8528=VERTEX_POINT ( 'NONE', #46339 ) ;
#8529=LINE ( 'NONE', #73840, #9538 ) ;
#8530=ORIENTED_EDGE ( 'NONE', *, *, #37133, .T. ) ;
#8531=ADVANCED_FACE ( 'NONE', ( #91931 ), #124572, .F. ) ;
#8532=CARTESIAN_POINT ( 'NONE',  ( 21.48921356237309155, -27.52281430457070499, 5.000000000000000000 ) ) ;
#8533=CARTESIAN_POINT ( 'NONE',  ( 16.49999999999989697, 5.696342897626525570, -7.587980461218362116 ) ) ;
#8536=ORIENTED_EDGE ( 'NONE', *, *, #33672, .T. ) ;
#8537=PLANE ( 'NONE',  #104292 ) ;
#8539=CARTESIAN_POINT ( 'NONE',  ( -9.005480084712511157, 28.92564299267931816, 4.000000000000000000 ) ) ;
#8541=ADVANCED_FACE ( 'NONE', ( #123880 ), #113687, .F. ) ;
#8543=DIRECTION ( 'NONE',  ( -0.7071067811865486830, -0.7071067811865464625, 0.000000000000000000 ) ) ;
#8544=ORIENTED_EDGE ( 'NONE', *, *, #58790, .T. ) ;
#8545=CARTESIAN_POINT ( 'NONE',  ( 0.000000000000000000, 0.000000000000000000, 5.000000000000000000 ) ) ;
#8546=VECTOR ( 'NONE', #91279, 1000.000000000000114 ) ;
#8548=CARTESIAN_POINT ( 'NONE',  ( -42.18398860626899705, 28.73617430169816700, 5.000000000000000000 ) ) ;
#8550=ORIENTED_EDGE ( 'NONE', *, *, #60724, .T. ) ;
#8551=EDGE_LOOP ( 'NONE', ( #102201, #135215, #82789, #34334 ) ) ;
#8552=ORIENTED_EDGE ( 'NONE', *, *, #41213, .F. ) ;
#8554=AXIS2_PLACEMENT_3D ( 'NONE', #67115, #1109, #134523 ) ;
#8555=ORIENTED_EDGE ( 'NONE', *, *, #6486, .T. ) ;
#8558=DIRECTION ( 'NONE',  ( -0.000000000000000000, -0.3543493200069152693, 0.9351131265310292928 ) ) ;
#8559=EDGE_LOOP ( 'NONE', ( #35310, #126674, #102379, #21360 ) ) ;
#8560=EDGE_CURVE ( 'NONE', #126893, #65352, #14381, .T. ) ;
#8562=DIRECTION ( 'NONE',  ( 0.7071067811865487940, 0.7071067811865463515, -0.000000000000000000 ) ) ;
#8564=ORIENTED_EDGE ( 'NONE', *, *, #44736, .T. ) ;
#8565=CARTESIAN_POINT ( 'NONE',  ( 33.29974487139158867, -27.71228299555229313, 4.000000000000000000 ) ) ;
#8566=DIRECTION ( 'NONE',  ( -0.7071067811865487940, 0.7071067811865463515, 0.000000000000000000 ) ) ;
#8567=VECTOR ( 'NONE', #102211, 1000.000000000000000 ) ;
#8568=DIRECTION ( 'NONE',  ( -0.7071067811865486830, -0.7071067811865464625, 0.000000000000000000 ) ) ;
#8569=CARTESIAN_POINT ( 'NONE',  ( -28.49999999999980460, -20.53675388469233098, 2.352720554255826713 ) ) ;
#8571=ORIENTED_EDGE ( 'NONE', *, *, #129435, .T. ) ;
#8574=CARTESIAN_POINT ( 'NONE',  ( 4.499999999999967137, -17.91344420646041868, 1.358650452708475287 ) ) ;
#8576=CARTESIAN_POINT ( 'NONE',  ( 16.56687199751246808, -21.74070752338406720, 6.915939825044033817 ) ) ;
#8577=CARTESIAN_POINT ( 'NONE',  ( 34.92499999999998295, 4.701930566820937685, 4.500000000000000888 ) ) ;
#8579=ADVANCED_FACE ( 'NONE', ( #4144 ), #92632, .F. ) ;
#8580=VERTEX_POINT ( 'NONE', #37577 ) ;
#8581=VECTOR ( 'NONE', #4476, 999.9999999999998863 ) ;
#8582=EDGE_LOOP ( 'NONE', ( #43104, #76849, #66591, #112566, #8550 ) ) ;
#8584=CARTESIAN_POINT ( 'NONE',  ( -69.48921356237309510, -27.52281430457103895, 5.000000000000000000 ) ) ;
#8585=ORIENTED_EDGE ( 'NONE', *, *, #100344, .F. ) ;
#8586=VERTEX_POINT ( 'NONE', #123163 ) ;
#8588=EDGE_CURVE ( 'NONE', #61667, #11699, #2779, .T. ) ;
#8589=DIRECTION ( 'NONE',  ( 1.000000000000000000, 0.000000000000000000, 0.000000000000000000 ) ) ;
#8590=DIRECTION ( 'NONE',  ( 0.6830127018922181881, 0.6830127018922202975, -0.2588190451025214056 ) ) ;
#8591=ORIENTED_EDGE ( 'NONE', *, *, #137345, .T. ) ;
#8592=CARTESIAN_POINT ( 'NONE',  ( -24.64318742751724045, -20.24070752338407786, 21.22881796311207481 ) ) ;
#8594=DIRECTION ( 'NONE',  ( -0.7071067811865486830, -0.7071067811865464625, 0.000000000000000000 ) ) ;
#8595=CARTESIAN_POINT ( 'NONE',  ( 24.89279686680829329, 1.949462372756121775, 4.672399651904028062 ) ) ;
#8599=EDGE_CURVE ( 'NONE', #34187, #5268, #57925, .T. ) ;
#8600=ORIENTED_EDGE ( 'NONE', *, *, #71170, .F. ) ;
#8602=CARTESIAN_POINT ( 'NONE',  ( 8.524873872149486331, 14.25929247661557575, 9.797011795316656446 ) ) ;
#8603=ORIENTED_EDGE ( 'NONE', *, *, #73097, .T. ) ;
#8604=ADVANCED_FACE ( 'NONE', ( #17905 ), #62912, .F. ) ;
#8605=EDGE_LOOP ( 'NONE', ( #57290, #17016, #31214, #81577 ) ) ;
#8607=ORIENTED_EDGE ( 'NONE', *, *, #66440, .F. ) ;
#8608=ORIENTED_EDGE ( 'NONE', *, *, #53571, .F. ) ;
#8610=EDGE_LOOP ( 'NONE', ( #106091, #21603, #110535 ) ) ;
#8611=AXIS2_PLACEMENT_3D ( 'NONE', #22693, #100308, #55382 ) ;
#8612=EDGE_CURVE ( 'NONE', #92353, #8845, #104949, .T. ) ;
#8613=VECTOR ( 'NONE', #31968, 1000.000000000000000 ) ;
#8615=DIRECTION ( 'NONE',  ( 0.3543493200069162685, -0.000000000000000000, -0.9351131265310288487 ) ) ;
#8618=PLANE ( 'NONE',  #5697 ) ;
#8619=LINE ( 'NONE', #140600, #4185 ) ;
#8620=LINE ( 'NONE', #140601, #87554 ) ;
#8623=ADVANCED_FACE ( 'NONE', ( #96196 ), #139024, .T. ) ;
#8624=CARTESIAN_POINT ( 'NONE',  ( -18.79289321881332597, 18.75929247661552068, 5.000000000000000000 ) ) ;
#8625=LINE ( 'NONE', #18826, #76061 ) ;
#8626=CARTESIAN_POINT ( 'NONE',  ( -48.29974487139158867, -27.71228299555239971, 4.000000000000000000 ) ) ;
#8627=CARTESIAN_POINT ( 'NONE',  ( 34.92499999999998295, 18.85612307739221549, 4.000000000000000000 ) ) ;
#8628=ORIENTED_EDGE ( 'NONE', *, *, #137477, .T. ) ;
#8629=EDGE_LOOP ( 'NONE', ( #114537, #102043, #6619, #114165 ) ) ;
#8630=EDGE_CURVE ( 'NONE', #79017, #101826, #40440, .T. ) ;
#8631=ORIENTED_EDGE ( 'NONE', *, *, #135943, .F. ) ;
#8633=FACE_OUTER_BOUND ( 'NONE', #54306, .T. ) ;
#8634=ORIENTED_EDGE ( 'NONE', *, *, #72710, .F. ) ;
#8635=EDGE_LOOP ( 'NONE', ( #101924, #114969, #92999, #103 ) ) ;
#8636=CARTESIAN_POINT ( 'NONE',  ( -33.48921356237309510, -27.52281430457078670, 5.000000000000000000 ) ) ;
#8637=PLANE ( 'NONE',  #108015 ) ;
#8638=DIRECTION ( 'NONE',  ( -0.7071067811865486830, -0.7071067811865464625, 0.000000000000000000 ) ) ;
#8640=VERTEX_POINT ( 'NONE', #17233 ) ;
#8641=VECTOR ( 'NONE', #33138, 999.9999999999998863 ) ;
#8642=ADVANCED_FACE ( 'NONE', ( #128159 ), #16496, .F. ) ;
#8643=CARTESIAN_POINT ( 'NONE',  ( 22.78501580275796101, -3.740707523384248390, 15.76143240460129569 ) ) ;
#8645=( BOUNDED_CURVE ( )  B_SPLINE_CURVE ( 3, ( #24199, #46721, #135130, #80042 ),
 .UNSPECIFIED., .F., .T. ) 
 B_SPLINE_CURVE_WITH_KNOTS ( ( 4, 4 ),
 ( 3.996889577052295195, 4.025035655492698261 ),
 .UNSPECIFIED. ) 
 CURVE ( )  GEOMETRIC_REPRESENTATION_ITEM ( )  RATIONAL_B_SPLINE_CURVE ( ( 1.000000000000000000, 0.9999339842785831545, 0.9999339842785831545, 1.000000000000000000 ) ) 
 REPRESENTATION_ITEM ( '' )  );
#8647=EDGE_CURVE ( 'NONE', #48148, #55125, #45055, .T. ) ;
#8648=PLANE ( 'NONE',  #14878 ) ;
#8649=VECTOR ( 'NONE', #105832, 999.9999999999998863 ) ;
#8651=ORIENTED_EDGE ( 'NONE', *, *, #52306, .F. ) ;
#8653=PLANE ( 'NONE',  #126907 ) ;
#8654=DIRECTION ( 'NONE',  ( -0.6830127018922180770, -0.6830127018922204085, -0.2588190451025213501 ) ) ;
#8655=DIRECTION ( 'NONE',  ( -0.7071067811865486830, -0.7071067811865464625, 0.000000000000000000 ) ) ;
#8656=EDGE_LOOP ( 'NONE', ( #43170, #108169, #52223, #67919 ) ) ;
#8657=ORIENTED_EDGE ( 'NONE', *, *, #128077, .T. ) ;
#8659=ORIENTED_EDGE ( 'NONE', *, *, #20126, .T. ) ;
#8660=LINE ( 'NONE', #119583, #138953 ) ;
#8661=DIRECTION ( 'NONE',  ( -0.7071067811865487940, 0.7071067811865463515, 0.000000000000000000 ) ) ;
#8662=CARTESIAN_POINT ( 'NONE',  ( -15.48921356237309510, -27.52281430457066236, 5.000000000000000000 ) ) ;
#8664=ORIENTED_EDGE ( 'NONE', *, *, #30388, .T. ) ;
#8665=DIRECTION ( 'NONE',  ( -0.000000000000000000, -0.3543493200069152693, 0.9351131265310292928 ) ) ;
#8666=FACE_OUTER_BOUND ( 'NONE', #18161, .T. ) ;
#8667=LINE ( 'NONE', #108707, #505 ) ;
#8669=DIRECTION ( 'NONE',  ( -0.000000000000000000, 0.000000000000000000, 1.000000000000000000 ) ) ;
#8671=EDGE_LOOP ( 'NONE', ( #42075, #124395, #43182, #127356 ) ) ;
#8673=VERTEX_POINT ( 'NONE', #60046 ) ;
#8674=ORIENTED_EDGE ( 'NONE', *, *, #128477, .T. ) ;
#8675=LINE ( 'NONE', #52921, #74843 ) ;
#8676=PLANE ( 'NONE',  #6655 ) ;
#8678=DIRECTION ( 'NONE',  ( -0.000000000000000000, -0.3543493200069152693, 0.9351131265310292928 ) ) ;
#8679=DIRECTION ( 'NONE',  ( -0.7071067811865486830, -0.7071067811865464625, 0.000000000000000000 ) ) ;
#8680=DIRECTION ( 'NONE',  ( 0.7071067811865486830, -0.7071067811865464625, -0.000000000000000000 ) ) ;
#8682=CARTESIAN_POINT ( 'NONE',  ( 44.99451991528749772, 28.92564299267969474, 4.000000000000000000 ) ) ;
#8683=CARTESIAN_POINT ( 'NONE',  ( 29.87852683662835318, -20.24070752338406720, 7.412974875817723408 ) ) ;
#8684=DIRECTION ( 'NONE',  ( -0.7071067811865486830, -0.7071067811865464625, 0.000000000000000000 ) ) ;
#8688=LINE ( 'NONE', #120319, #90701 ) ;
#8689=CARTESIAN_POINT ( 'NONE',  ( -30.18398860626900060, 28.73617430169808173, 5.000000000000000000 ) ) ;
#8691=CARTESIAN_POINT ( 'NONE',  ( 30.48921356237309510, -27.52281430457076894, 5.000000000000000000 ) ) ;
#8692=VERTEX_POINT ( 'NONE', #39728 ) ;
#8693=ORIENTED_EDGE ( 'NONE', *, *, #139898, .F. ) ;
#8694=EDGE_LOOP ( 'NONE', ( #18744, #61084, #111096, #23073, #125773, #60748 ) ) ;
#8696=AXIS2_PLACEMENT_3D ( 'NONE', #119124, #105386, #8191 ) ;
#8697=ORIENTED_EDGE ( 'NONE', *, *, #21759, .T. ) ;
#8699=EDGE_CURVE ( 'NONE', #33874, #94223, #104211, .T. ) ;
#8700=EDGE_LOOP ( 'NONE', ( #48876, #104785, #30455, #86391 ) ) ;
#8701=CARTESIAN_POINT ( 'NONE',  ( 10.49999999999992184, 19.39370406404967895, 1.459788787078177830 ) ) ;
#8702=LINE ( 'NONE', #51571, #43966 ) ;
#8703=ORIENTED_EDGE ( 'NONE', *, *, #86153, .F. ) ;
#8704=VECTOR ( 'NONE', #24384, 1000.000000000000000 ) ;
#8705=DIRECTION ( 'NONE',  ( 0.000000000000000000, 1.000000000000000000, -0.000000000000000000 ) ) ;
#8706=LINE ( 'NONE', #116084, #76617 ) ;
#8708=DIRECTION ( 'NONE',  ( -0.7071067811865486830, -0.7071067811865464625, -0.000000000000000000 ) ) ;
#8709=DIRECTION ( 'NONE',  ( 0.7071067811865486830, -0.7071067811865464625, -0.000000000000000000 ) ) ;
#8711=EDGE_CURVE ( 'NONE', #142010, #33645, #1443, .T. ) ;
#8712=ORIENTED_EDGE ( 'NONE', *, *, #1520, .F. ) ;
#8714=EDGE_CURVE ( 'NONE', #8442, #11462, #85327, .T. ) ;
#8716=VECTOR ( 'NONE', #140671, 999.9999999999998863 ) ;
#8717=DIRECTION ( 'NONE',  ( -0.000000000000000000, 0.3543493200069153248, 0.9351131265310292928 ) ) ;
#8718=CARTESIAN_POINT ( 'NONE',  ( -45.48921356237309510, -27.52281430457087197, 5.000000000000000000 ) ) ;
#8719=CARTESIAN_POINT ( 'NONE',  ( 63.29974487139158867, -27.71228299555250274, 4.000000000000000000 ) ) ;
#8721=CARTESIAN_POINT ( 'NONE',  ( -1.251544128675743828, -11.24070752338416845, 10.39518518046009632 ) ) ;
#8722=ORIENTED_EDGE ( 'NONE', *, *, #112900, .T. ) ;
#8725=VERTEX_POINT ( 'NONE', #6298 ) ;
#8726=EDGE_CURVE ( 'NONE', #75249, #6819, #49175, .T. ) ;
#8727=DIRECTION ( 'NONE',  ( -0.3543493200069163240, -0.000000000000000000, -0.9351131265310288487 ) ) ;
#8728=DIRECTION ( 'NONE',  ( 0.6830127018922181881, 0.6830127018922202975, -0.2588190451025214056 ) ) ;
#8729=CARTESIAN_POINT ( 'NONE',  ( -34.92500000000001137, 22.22500000000000142, 4.000000000000000000 ) ) ;
#8730=CARTESIAN_POINT ( 'NONE',  ( -15.92034494338828665, -22.22500000000000142, 12.20157423226259397 ) ) ;
#8731=EDGE_CURVE ( 'NONE', #87168, #32802, #38283, .T. ) ;
#8732=LINE ( 'NONE', #141448, #30435 ) ;
#8733=DIRECTION ( 'NONE',  ( 0.7071067811865487940, 0.7071067811865463515, 0.000000000000000000 ) ) ;
#8735=ORIENTED_EDGE ( 'NONE', *, *, #63175, .T. ) ;
#8736=DIRECTION ( 'NONE',  ( -0.6830127018922181881, 0.6830127018922202975, -0.2588190451025214056 ) ) ;
#8737=ORIENTED_EDGE ( 'NONE', *, *, #93219, .F. ) ;
#8738=LINE ( 'NONE', #109536, #36935 ) ;
#8739=EDGE_CURVE ( 'NONE', #91902, #120409, #82500, .T. ) ;
#8740=EDGE_CURVE ( 'NONE', #132281, #19758, #105642, .T. ) ;
#8741=LINE ( 'NONE', #17520, #4651 ) ;
#8742=PLANE ( 'NONE',  #88164 ) ;
#8743=ORIENTED_EDGE ( 'NONE', *, *, #119718, .F. ) ;
#8746=PLANE ( 'NONE',  #28524 ) ;
#8747=LINE ( 'NONE', #74070, #32293 ) ;
#8748=CARTESIAN_POINT ( 'NONE',  ( 15.79289321881334907, -20.24070752338407431, 5.000000000000000000 ) ) ;
#8750=DIRECTION ( 'NONE',  ( -0.000000000000000000, -0.3543493200069153248, -0.9351131265310291818 ) ) ;
#8752=VERTEX_POINT ( 'NONE', #49889 ) ;
#8753=ADVANCED_FACE ( 'NONE', ( #129550 ), #94068, .F. ) ;
#8754=DIRECTION ( 'NONE',  ( 0.7071067811865487940, 0.7071067811865463515, 0.000000000000000000 ) ) ;
#8755=ORIENTED_EDGE ( 'NONE', *, *, #9622, .F. ) ;
#8756=EDGE_LOOP ( 'NONE', ( #6229, #133803, #45795 ) ) ;
#8757=VERTEX_POINT ( 'NONE', #94772 ) ;
#8758=AXIS2_PLACEMENT_3D ( 'NONE', #56911, #4564, #35876 ) ;
#8759=ADVANCED_FACE ( 'NONE', ( #78059 ), #107789, .F. ) ;
#8761=CARTESIAN_POINT ( 'NONE',  ( -5.816011393731002066, 28.73617430169783304, 5.000000000000000000 ) ) ;
#8762=EDGE_LOOP ( 'NONE', ( #128751, #38826, #102910, #1522 ) ) ;
#8763=DIRECTION ( 'NONE',  ( 0.7071067811865486830, -0.7071067811865464625, -0.000000000000000000 ) ) ;
#8764=CARTESIAN_POINT ( 'NONE',  ( 12.00548008471251293, 28.92564299267929684, 4.000000000000000000 ) ) ;
#8765=ADVANCED_FACE ( 'NONE', ( #52703 ), #141897, .F. ) ;
#8766=CARTESIAN_POINT ( 'NONE',  ( -25.82816939922334853, -11.24070752338417201, 4.000000000000000000 ) ) ;
#8767=FACE_BOUND ( 'NONE', #128720, .T. ) ;
#8768=EDGE_CURVE ( 'NONE', #34652, #28496, #42591, .T. ) ;
#8769=ORIENTED_EDGE ( 'NONE', *, *, #134186, .F. ) ;
#8770=CARTESIAN_POINT ( 'NONE',  ( 20.99451991528748707, 28.92564299267952777, 4.000000000000000000 ) ) ;
#8771=PLANE ( 'NONE',  #81521 ) ;
#8772=FACE_OUTER_BOUND ( 'NONE', #133917, .T. ) ;
#8774=ORIENTED_EDGE ( 'NONE', *, *, #13487, .F. ) ;
#8775=LINE ( 'NONE', #107428, #89785 ) ;
#8777=EDGE_LOOP ( 'NONE', ( #48900, #58557, #87689, #133171 ) ) ;
#8778=DIRECTION ( 'NONE',  ( -0.6830127018922181881, 0.6830127018922202975, -0.2588190451025214056 ) ) ;
#8779=ORIENTED_EDGE ( 'NONE', *, *, #33104, .F. ) ;
#8781=EDGE_LOOP ( 'NONE', ( #50927, #29912, #86541, #77466 ) ) ;
#8782=AXIS2_PLACEMENT_3D ( 'NONE', #116187, #93726, #126344 ) ;
#8783=ADVANCED_FACE ( 'NONE', ( #105154 ), #17425, .F. ) ;
#8784=CARTESIAN_POINT ( 'NONE',  ( 18.48921356237309510, -27.52281430457068367, 5.000000000000000000 ) ) ;
#8786=ORIENTED_EDGE ( 'NONE', *, *, #44381, .T. ) ;
#8787=CARTESIAN_POINT ( 'NONE',  ( 39.18398860626899705, 28.73617430169814568, 5.000000000000000000 ) ) ;
#8788=CARTESIAN_POINT ( 'NONE',  ( 2.700255128608413990, -27.71228299555204089, 4.000000000000000000 ) ) ;
#8789=EDGE_CURVE ( 'NONE', #136335, #23129, #26182, .T. ) ;
#8792=FACE_OUTER_BOUND ( 'NONE', #115300, .T. ) ;
#8794=CARTESIAN_POINT ( 'NONE',  ( 13.49999999999990763, 10.94296225409028089, -9.576120664313226172 ) ) ;
#8795=VERTEX_POINT ( 'NONE', #126202 ) ;
#8796=VERTEX_POINT ( 'NONE', #103022 ) ;
#8797=CARTESIAN_POINT ( 'NONE',  ( -7.954842266633281866, -21.74070752338405299, 21.72585301388582479 ) ) ;
#8798=AXIS2_PLACEMENT_3D ( 'NONE', #46377, #56551, #111584 ) ;
#8800=ORIENTED_EDGE ( 'NONE', *, *, #19312, .T. ) ;
#8801=VERTEX_POINT ( 'NONE', #71846 ) ;
#8802=VECTOR ( 'NONE', #130262, 1000.000000000000227 ) ;
#8803=ORIENTED_EDGE ( 'NONE', *, *, #106297, .T. ) ;
#8804=CARTESIAN_POINT ( 'NONE',  ( -34.92500000000001137, 22.22500000000000142, 4.500000000000000888 ) ) ;
#8805=CARTESIAN_POINT ( 'NONE',  ( 11.70025512860841133, -27.71228299555198049, 4.000000000000000000 ) ) ;
#8806=ORIENTED_EDGE ( 'NONE', *, *, #17645, .F. ) ;
#8807=LINE ( 'NONE', #41488, #37064 ) ;
#8808=VECTOR ( 'NONE', #126000, 999.9999999999998863 ) ;
#8809=VECTOR ( 'NONE', #89780, 1000.000000000000000 ) ;
#8810=EDGE_CURVE ( 'NONE', #129287, #72440, #50082, .T. ) ;
#8811=LINE ( 'NONE', #42950, #137053 ) ;
#8814=DIRECTION ( 'NONE',  ( -0.6830127018922180770, -0.6830127018922204085, -0.2588190451025213501 ) ) ;
#8815=ORIENTED_EDGE ( 'NONE', *, *, #29172, .F. ) ;
#8817=FACE_OUTER_BOUND ( 'NONE', #42027, .T. ) ;
#8818=DIRECTION ( 'NONE',  ( 1.000000000000000000, 0.000000000000000000, 0.000000000000000000 ) ) ;
#8819=VERTEX_POINT ( 'NONE', #103697 ) ;
#8821=CARTESIAN_POINT ( 'NONE',  ( -26.24139925780185578, 21.72500000000000142, 5.000000000000000000 ) ) ;
#8822=VERTEX_POINT ( 'NONE', #69708 ) ;
#8824=DIRECTION ( 'NONE',  ( -0.7071067811865486830, -0.7071067811865464625, 0.000000000000000000 ) ) ;
#8825=DIRECTION ( 'NONE',  ( -0.6830127018922181881, 0.6830127018922202975, -0.2588190451025214056 ) ) ;
#8826=EDGE_LOOP ( 'NONE', ( #119878, #29970, #138476, #57453 ) ) ;
#8828=DIRECTION ( 'NONE',  ( -0.3543493200069163240, 4.681814790819596721E-17, -0.9351131265310288487 ) ) ;
#8830=VECTOR ( 'NONE', #104294, 999.9999999999998863 ) ;
#8831=DIRECTION ( 'NONE',  ( -0.7071067811865487940, 0.7071067811865463515, 0.000000000000000000 ) ) ;
#8834=VERTEX_POINT ( 'NONE', #5090 ) ;
#8835=VECTOR ( 'NONE', #86957, 999.9999999999998863 ) ;
#8837=FACE_OUTER_BOUND ( 'NONE', #52166, .T. ) ;
#8839=ORIENTED_EDGE ( 'NONE', *, *, #94197, .F. ) ;
#8840=DIRECTION ( 'NONE',  ( -0.7071067811865486830, 0.7071067811865464625, 0.000000000000000000 ) ) ;
#8841=LINE ( 'NONE', #132134, #82991 ) ;
#8843=LINE ( 'NONE', #11732, #87820 ) ;
#8844=DIRECTION ( 'NONE',  ( 0.7071067811865487940, 0.7071067811865463515, 0.000000000000000000 ) ) ;
#8845=VERTEX_POINT ( 'NONE', #136353 ) ;
#8847=DIRECTION ( 'NONE',  ( 0.7071067811865486830, -0.7071067811865464625, -0.000000000000000000 ) ) ;
#8848=CARTESIAN_POINT ( 'NONE',  ( 8.999999999999937828, -18.41253812416056590, 4.000000000000000000 ) ) ;
#8849=VECTOR ( 'NONE', #19546, 1000.000000000000227 ) ;
#8850=DIRECTION ( 'NONE',  ( 0.6830127018922180770, -0.6830127018922204085, -0.2588190451025213501 ) ) ;
#8852=VECTOR ( 'NONE', #97313, 1000.000000000000000 ) ;
#8853=VERTEX_POINT ( 'NONE', #49390 ) ;
#8854=LINE ( 'NONE', #28553, #55704 ) ;
#8855=ORIENTED_EDGE ( 'NONE', *, *, #42669, .T. ) ;
#8856=ORIENTED_EDGE ( 'NONE', *, *, #116781, .T. ) ;
#8857=CARTESIAN_POINT ( 'NONE',  ( 13.49999999999990585, 15.05218569542901186, 5.000000000000000000 ) ) ;
#8858=CARTESIAN_POINT ( 'NONE',  ( 0.000000000000000000, 0.000000000000000000, 5.000000000000000000 ) ) ;
#8859=ORIENTED_EDGE ( 'NONE', *, *, #139058, .F. ) ;
#8860=CARTESIAN_POINT ( 'NONE',  ( 7.499999999999951150, -4.216083040037250207, -7.486842126848674894 ) ) ;
#8861=EDGE_CURVE ( 'NONE', #34748, #31094, #58861, .T. ) ;
#8862=LINE ( 'NONE', #63355, #85677 ) ;
#8863=LINE ( 'NONE', #62616, #27972 ) ;
#8864=DIRECTION ( 'NONE',  ( -0.7071067811865487940, 0.7071067811865463515, -0.000000000000000000 ) ) ;
#8865=EDGE_CURVE ( 'NONE', #20167, #64959, #126884, .T. ) ;
#8866=ADVANCED_FACE ( 'NONE', ( #6502 ), #114589, .T. ) ;
#8867=ORIENTED_EDGE ( 'NONE', *, *, #126387, .F. ) ;
#8868=DIRECTION ( 'NONE',  ( -0.000000000000000000, 0.3543493200069153248, 0.9351131265310292928 ) ) ;
#8869=CARTESIAN_POINT ( 'NONE',  ( 14.99999999999989519, -8.151047557385055597, -8.977947279169832484 ) ) ;
#8871=LINE ( 'NONE', #132169, #133561 ) ;
#8872=DIRECTION ( 'NONE',  ( -0.7071067811865486830, -0.7071067811865464625, 0.000000000000000000 ) ) ;
#8875=EDGE_CURVE ( 'NONE', #83448, #74127, #130203, .T. ) ;
#8877=ADVANCED_FACE ( 'NONE', ( #39939 ), #104429, .F. ) ;
#8878=CARTESIAN_POINT ( 'NONE',  ( 14.99451991528749595, 28.92564299267948513, 4.000000000000000000 ) ) ;
#8879=ORIENTED_EDGE ( 'NONE', *, *, #87587, .T. ) ;
#8880=EDGE_LOOP ( 'NONE', ( #135748, #8150, #90347, #90355 ) ) ;
#8883=EDGE_CURVE ( 'NONE', #41257, #33380, #116744, .T. ) ;
#8884=LINE ( 'NONE', #64054, #76391 ) ;
#8885=FACE_OUTER_BOUND ( 'NONE', #36025, .T. ) ;
#8886=ORIENTED_EDGE ( 'NONE', *, *, #88573, .F. ) ;
#8887=LINE ( 'NONE', #43725, #81622 ) ;
#8889=VECTOR ( 'NONE', #105171, 1000.000000000000000 ) ;
#8892=CARTESIAN_POINT ( 'NONE',  ( 48.48921356237309510, -27.52281430457089328, 5.000000000000000000 ) ) ;
#8893=ORIENTED_EDGE ( 'NONE', *, *, #56610, .T. ) ;
#8894=EDGE_LOOP ( 'NONE', ( #94877, #4419, #8203, #105936 ) ) ;
#8895=LINE ( 'NONE', #141633, #26372 ) ;
#8898=VECTOR ( 'NONE', #86099, 1000.000000000000000 ) ;
#8900=CARTESIAN_POINT ( 'NONE',  ( 24.48921356237309510, -27.52281430457072631, 5.000000000000000000 ) ) ;
#8903=DIRECTION ( 'NONE',  ( -0.7071067811865487940, 0.7071067811865463515, -0.000000000000000000 ) ) ;
#8904=ORIENTED_EDGE ( 'NONE', *, *, #31105, .F. ) ;
#8907=ORIENTED_EDGE ( 'NONE', *, *, #102156, .F. ) ;
#8909=DIRECTION ( 'NONE',  ( 0.7071067811865486830, -0.7071067811865464625, -0.000000000000000000 ) ) ;
#8910=LINE ( 'NONE', #108975, #52335 ) ;
#8912=EDGE_CURVE ( 'NONE', #9095, #112404, #115271, .T. ) ;
#8913=VECTOR ( 'NONE', #13814, 1000.000000000000000 ) ;
#8914=VECTOR ( 'NONE', #9591, 1000.000000000000000 ) ;
#8915=ORIENTED_EDGE ( 'NONE', *, *, #39966, .T. ) ;
#8917=CARTESIAN_POINT ( 'NONE',  ( 30.48921356237309510, -27.52281430457076894, 5.000000000000000000 ) ) ;
#8918=ADVANCED_FACE ( 'NONE', ( #15961 ), #82704, .T. ) ;
#8920=CARTESIAN_POINT ( 'NONE',  ( 21.18398860626899349, 28.73617430169802134, 5.000000000000000000 ) ) ;
#8921=ORIENTED_EDGE ( 'NONE', *, *, #93878, .F. ) ;
#8922=EDGE_LOOP ( 'NONE', ( #15671, #67477, #128647, #42909 ) ) ;
#8923=AXIS2_PLACEMENT_3D ( 'NONE', #6535, #69748, #3692 ) ;
#8924=CARTESIAN_POINT ( 'NONE',  ( 42.18398860626899705, 28.73617430169816700, 5.000000000000000000 ) ) ;
#8925=CARTESIAN_POINT ( 'NONE',  ( 0.000000000000000000, 0.000000000000000000, 0.000000000000000000 ) ) ;
#8926=ORIENTED_EDGE ( 'NONE', *, *, #26089, .T. ) ;
#8927=ADVANCED_FACE ( 'NONE', ( #98557 ), #18105, .F. ) ;
#8930=DIRECTION ( 'NONE',  ( -0.7071067811865486830, -0.7071067811865464625, -0.000000000000000000 ) ) ;
#8931=VERTEX_POINT ( 'NONE', #119571 ) ;
#8932=EDGE_CURVE ( 'NONE', #30215, #14718, #20267, .T. ) ;
#8933=CARTESIAN_POINT ( 'NONE',  ( -18.79289321881332242, 15.75929247661555976, 5.000000000000000000 ) ) ;
#8934=LINE ( 'NONE', #128640, #133590 ) ;
#8935=VECTOR ( 'NONE', #52249, 1000.000000000000000 ) ;
#8936=VECTOR ( 'NONE', #102760, 1000.000000000000000 ) ;
#8937=AXIS2_PLACEMENT_3D ( 'NONE', #139817, #17283, #61546 ) ;
#8939=DIRECTION ( 'NONE',  ( 0.7071067811865487940, 0.7071067811865463515, -0.000000000000000000 ) ) ;
#8941=FACE_BOUND ( 'NONE', #18511, .T. ) ;
#8942=CARTESIAN_POINT ( 'NONE',  ( -34.92500000000001137, 13.70193056682087196, 4.500000000000000888 ) ) ;
#8944=DIRECTION ( 'NONE',  ( -0.000000000000000000, 0.3543493200069153248, 0.9351131265310292928 ) ) ;
#8945=CARTESIAN_POINT ( 'NONE',  ( 28.49999999999981171, 1.030536316426539756, -5.498701923753864129 ) ) ;
#8946=ORIENTED_EDGE ( 'NONE', *, *, #23148, .T. ) ;
#8947=VECTOR ( 'NONE', #63860, 1000.000000000000000 ) ;
#8948=CIRCLE ( 'NONE', #43784, 5.968999999999998529 ) ;
#8951=ORIENTED_EDGE ( 'NONE', *, *, #104545, .F. ) ;
#8952=EDGE_LOOP ( 'NONE', ( #110995, #37352, #86233, #4895 ) ) ;
#8954=ORIENTED_EDGE ( 'NONE', *, *, #31238, .F. ) ;
#8955=ADVANCED_FACE ( 'NONE', ( #53645 ), #8648, .F. ) ;
#8956=CARTESIAN_POINT ( 'NONE',  ( 11.99999999999991473, -16.60178936734447319, 0.8616154019347775916 ) ) ;
#8958=PLANE ( 'NONE',  #7320 ) ;
#8960=EDGE_CURVE ( 'NONE', #30662, #19069, #75397, .T. ) ;
#8961=LINE ( 'NONE', #98866, #86522 ) ;
#8962=CARTESIAN_POINT ( 'NONE',  ( 30.18398860626900060, 28.73617430169808173, 5.000000000000000000 ) ) ;
#8963=LINE ( 'NONE', #41643, #50154 ) ;
#8964=CARTESIAN_POINT ( 'NONE',  ( 30.48921356237309510, -27.52281430457076894, 5.000000000000000000 ) ) ;
#8965=CARTESIAN_POINT ( 'NONE',  ( -5.816011393731002066, 28.73617430169783304, 5.000000000000000000 ) ) ;
#8966=LINE ( 'NONE', #120615, #639 ) ;
#8967=CARTESIAN_POINT ( 'NONE',  ( -45.48921356237309510, -27.52281430457087197, 5.000000000000000000 ) ) ;
#8968=ORIENTED_EDGE ( 'NONE', *, *, #89026, .T. ) ;
#8971=CARTESIAN_POINT ( 'NONE',  ( -7.499999999999951150, -1.592773361805382981, -6.492772025301212224 ) ) ;
#8972=CARTESIAN_POINT ( 'NONE',  ( -19.69064382391260892, -2.759520746520534473, 4.000000000000000000 ) ) ;
#8973=EDGE_LOOP ( 'NONE', ( #76087, #18538, #115063, #20846 ) ) ;
#8975=ORIENTED_EDGE ( 'NONE', *, *, #54200, .T. ) ;
#8976=DIRECTION ( 'NONE',  ( -0.6830127018922181881, 0.6830127018922202975, -0.2588190451025214056 ) ) ;
#8977=VERTEX_POINT ( 'NONE', #131195 ) ;
#8978=EDGE_CURVE ( 'NONE', #80320, #113825, #95702, .T. ) ;
#8980=ORIENTED_EDGE ( 'NONE', *, *, #39841, .F. ) ;
#8981=CARTESIAN_POINT ( 'NONE',  ( 0.2997448713915885632, -27.71228299555206220, 4.000000000000000000 ) ) ;
#8982=EDGE_CURVE ( 'NONE', #7797, #54723, #130502, .T. ) ;
#8985=ORIENTED_EDGE ( 'NONE', *, *, #44533, .F. ) ;
#8986=FACE_OUTER_BOUND ( 'NONE', #34806, .T. ) ;
#8987=ORIENTED_EDGE ( 'NONE', *, *, #109740, .F. ) ;
#8988=LINE ( 'NONE', #141718, #48817 ) ;
#8989=PLANE ( 'NONE',  #1193 ) ;
#8990=LINE ( 'NONE', #140973, #77203 ) ;
#8991=ORIENTED_EDGE ( 'NONE', *, *, #19128, .F. ) ;
#8992=ORIENTED_EDGE ( 'NONE', *, *, #73139, .T. ) ;
#8993=CARTESIAN_POINT ( 'NONE',  ( 25.82816939922335209, -2.240707523384257716, 4.000000000000000000 ) ) ;
#8994=CARTESIAN_POINT ( 'NONE',  ( 33.41161490594808470, 22.22500000000000497, 4.777194822843814137 ) ) ;
#8995=VERTEX_POINT ( 'NONE', #65253 ) ;
#8996=EDGE_CURVE ( 'NONE', #63176, #30783, #118881, .T. ) ;
#8999=ORIENTED_EDGE ( 'NONE', *, *, #17802, .T. ) ;
#9000=EDGE_LOOP ( 'NONE', ( #53952, #81698, #2936, #52833 ) ) ;
#9002=VECTOR ( 'NONE', #108797, 1000.000000000000000 ) ;
#9003=VECTOR ( 'NONE', #143103, 999.9999999999998863 ) ;
#9005=VECTOR ( 'NONE', #82279, 999.9999999999998863 ) ;
#9006=DIRECTION ( 'NONE',  ( -0.7071067811865486830, 0.7071067811865464625, 0.000000000000000000 ) ) ;
#9008=FACE_OUTER_BOUND ( 'NONE', #44273, .T. ) ;
#9010=DIRECTION ( 'NONE',  ( -0.000000000000000000, 0.000000000000000000, 1.000000000000000000 ) ) ;
#9012=EDGE_CURVE ( 'NONE', #98151, #57105, #29029, .T. ) ;
#9013=ORIENTED_EDGE ( 'NONE', *, *, #123635, .F. ) ;
#9014=FACE_OUTER_BOUND ( 'NONE', #102365, .T. ) ;
#9016=VECTOR ( 'NONE', #47308, 1000.000000000000000 ) ;
#9017=LINE ( 'NONE', #131575, #10030 ) ;
#9018=CARTESIAN_POINT ( 'NONE',  ( -7.294715974614694787, 22.22500000000000142, -5.470147491473989376 ) ) ;
#9019=EDGE_LOOP ( 'NONE', ( #70328, #10169, #89993, #64466 ) ) ;
#9020=PLANE ( 'NONE',  #136339 ) ;
#9022=CARTESIAN_POINT ( 'NONE',  ( -5.816011393731002066, 28.73617430169783304, 5.000000000000000000 ) ) ;
#9024=VERTEX_POINT ( 'NONE', #31882 ) ;
#9025=LINE ( 'NONE', #119255, #99806 ) ;
#9026=DIRECTION ( 'NONE',  ( -0.6830127018922180770, -0.6830127018922204085, -0.2588190451025213501 ) ) ;
#9027=VECTOR ( 'NONE', #71525, 999.9999999999998863 ) ;
#9028=VECTOR ( 'NONE', #41694, 1000.000000000000000 ) ;
#9029=PLANE ( 'NONE',  #47419 ) ;
#9032=PLANE ( 'NONE',  #95079 ) ;
#9033=AXIS2_PLACEMENT_3D ( 'NONE', #35010, #56786, #100944 ) ;
#9034=PLANE ( 'NONE',  #136478 ) ;
#9036=CARTESIAN_POINT ( 'NONE',  ( -26.20666063542134339, 21.75929247661549226, 4.998822639870711626 ) ) ;
#9037=ORIENTED_EDGE ( 'NONE', *, *, #117897, .F. ) ;
#9039=EDGE_CURVE ( 'NONE', #94283, #16938, #84835, .T. ) ;
#9040=ORIENTED_EDGE ( 'NONE', *, *, #118092, .T. ) ;
#9041=PLANE ( 'NONE',  #33888 ) ;
#9042=ORIENTED_EDGE ( 'NONE', *, *, #95731, .T. ) ;
#9043=VECTOR ( 'NONE', #120008, 1000.000000000000000 ) ;
#9046=CARTESIAN_POINT ( 'NONE',  ( -15.16464500931035886, 22.22500000000000142, -2.487937186831706171 ) ) ;
#9049=LINE ( 'NONE', #129448, #2247 ) ;
#9050=DIRECTION ( 'NONE',  ( -0.6830127018922181881, 0.6830127018922202975, -0.2588190451025214056 ) ) ;
#9051=FACE_OUTER_BOUND ( 'NONE', #10367, .T. ) ;
#9052=EDGE_CURVE ( 'NONE', #84184, #122293, #137634, .T. ) ;
#9053=EDGE_CURVE ( 'NONE', #28495, #64833, #97089, .T. ) ;
#9055=ORIENTED_EDGE ( 'NONE', *, *, #37158, .F. ) ;
#9056=LINE ( 'NONE', #65688, #64889 ) ;
#9057=CARTESIAN_POINT ( 'NONE',  ( 26.20710678118636139, 6.759292476615649470, 5.000000000000000000 ) ) ;
#9060=LINE ( 'NONE', #40345, #26457 ) ;
#9061=CARTESIAN_POINT ( 'NONE',  ( 34.42499999999998295, 4.541399257802000378, 5.000000000000000000 ) ) ;
#9062=EDGE_CURVE ( 'NONE', #10646, #94260, #141347, .T. ) ;
#9064=EDGE_CURVE ( 'NONE', #29147, #1156, #45951, .T. ) ;
#9065=DIRECTION ( 'NONE',  ( 0.7071067811865487940, -0.7071067811865463515, 0.000000000000000000 ) ) ;
#9066=DIRECTION ( 'NONE',  ( -0.7071067811865487940, 0.7071067811865463515, 0.000000000000000000 ) ) ;
#9067=ORIENTED_EDGE ( 'NONE', *, *, #113032, .T. ) ;
#9068=ADVANCED_FACE ( 'NONE', ( #86278 ), #118141, .T. ) ;
#9069=FACE_OUTER_BOUND ( 'NONE', #57568, .T. ) ;
#9070=ADVANCED_FACE ( 'NONE', ( #43474 ), #131920, .F. ) ;
#9073=VECTOR ( 'NONE', #7445, 1000.000000000000000 ) ;
#9074=ADVANCED_FACE ( 'NONE', ( #57059 ), #26539, .F. ) ;
#9076=CARTESIAN_POINT ( 'NONE',  ( 56.99451991528749062, 28.92564299267978001, 4.000000000000000000 ) ) ;
#9077=ADVANCED_FACE ( 'NONE', ( #47619 ), #134610, .F. ) ;
#9078=EDGE_LOOP ( 'NONE', ( #62355, #100063, #32421, #57588 ) ) ;
#9080=CARTESIAN_POINT ( 'NONE',  ( 72.48921356237309510, -27.52281430457106026, 5.000000000000000000 ) ) ;
#9081=FACE_OUTER_BOUND ( 'NONE', #22407, .T. ) ;
#9082=EDGE_LOOP ( 'NONE', ( #969, #23057, #117965, #75357 ) ) ;
#9083=CARTESIAN_POINT ( 'NONE',  ( -11.00492477221187393, -5.240707523384228850, 12.38332538355498436 ) ) ;
#9085=CARTESIAN_POINT ( 'NONE',  ( -11.99999999999992006, -10.06887692260771239, 4.000000000000000000 ) ) ;
#9087=CARTESIAN_POINT ( 'NONE',  ( -10.44665057663211449, 2.259292476615697876, 14.86850063742356909 ) ) ;
#9088=CARTESIAN_POINT ( 'NONE',  ( -32.29289321881322650, 8.259292476615637923, 5.000000000000000000 ) ) ;
#9089=EDGE_LOOP ( 'NONE', ( #106158, #28871, #95644, #58097 ) ) ;
#9090=CARTESIAN_POINT ( 'NONE',  ( 5.206660635421493488, 21.75929247661549937, 4.998822639870701856 ) ) ;
#9091=CARTESIAN_POINT ( 'NONE',  ( -13.82334089840018443, 5.259292476615659240, 15.86257073897100867 ) ) ;
#9092=EDGE_CURVE ( 'NONE', #35675, #120153, #123733, .T. ) ;
#9093=LINE ( 'NONE', #44680, #73851 ) ;
#9095=VERTEX_POINT ( 'NONE', #70094 ) ;
#9097=ORIENTED_EDGE ( 'NONE', *, *, #29054, .T. ) ;
#9098=LINE ( 'NONE', #53366, #1277 ) ;
#9099=CARTESIAN_POINT ( 'NONE',  ( -19.11017322888196901, -22.22499999999999432, 4.785647885939354751 ) ) ;
#9100=DIRECTION ( 'NONE',  ( 0.7071067811865486830, -0.7071067811865464625, -0.000000000000000000 ) ) ;
#9101=CARTESIAN_POINT ( 'NONE',  ( -59.99451991528749772, 28.92564299267980132, 4.000000000000000000 ) ) ;
#9103=LINE ( 'NONE', #97584, #90887 ) ;
#9107=CARTESIAN_POINT ( 'NONE',  ( -31.49999999999977973, -19.91253812416054814, 4.000000000000000000 ) ) ;
#9108=EDGE_CURVE ( 'NONE', #87703, #71573, #15608, .T. ) ;
#9109=CARTESIAN_POINT ( 'NONE',  ( 5.994519915287488843, 28.92564299267942118, 4.000000000000000000 ) ) ;
#9110=CARTESIAN_POINT ( 'NONE',  ( 26.20710678118636139, -2.240707523384257716, 5.000000000000000000 ) ) ;
#9111=AXIS2_PLACEMENT_3D ( 'NONE', #42235, #106006, #131365 ) ;
#9112=AXIS2_PLACEMENT_3D ( 'NONE', #91790, #113535, #58521 ) ;
#9113=AXIS2_PLACEMENT_3D ( 'NONE', #73887, #74617, #105765 ) ;
#9114=EDGE_CURVE ( 'NONE', #42222, #114028, #123002, .T. ) ;
#9115=VERTEX_POINT ( 'NONE', #14930 ) ;
#9116=ORIENTED_EDGE ( 'NONE', *, *, #76782, .F. ) ;
#9117=CARTESIAN_POINT ( 'NONE',  ( 56.99451991528749062, 28.92564299267978001, 4.000000000000000000 ) ) ;
#9118=CARTESIAN_POINT ( 'NONE',  ( -60.29974487139158867, -27.71228299555248142, 4.000000000000000000 ) ) ;
#9119=LINE ( 'NONE', #66427, #127541 ) ;
#9123=ORIENTED_EDGE ( 'NONE', *, *, #67424, .F. ) ;
#9124=VECTOR ( 'NONE', #48850, 1000.000000000000114 ) ;
#9125=VERTEX_POINT ( 'NONE', #37423 ) ;
#9127=ORIENTED_EDGE ( 'NONE', *, *, #52558, .T. ) ;
#9128=EDGE_CURVE ( 'NONE', #22009, #57196, #12782, .T. ) ;
#9129=ORIENTED_EDGE ( 'NONE', *, *, #73652, .F. ) ;
#9130=AXIS2_PLACEMENT_3D ( 'NONE', #42129, #52260, #142847 ) ;
#9131=VECTOR ( 'NONE', #140754, 1000.000000000000000 ) ;
#9133=LINE ( 'NONE', #66444, #133467 ) ;
#9134=VECTOR ( 'NONE', #110032, 1000.000000000000114 ) ;
#9135=DIRECTION ( 'NONE',  ( 0.7071067811865487940, -0.7071067811865463515, 0.000000000000000000 ) ) ;
#9136=ORIENTED_EDGE ( 'NONE', *, *, #28622, .T. ) ;
#9137=DIRECTION ( 'NONE',  ( -0.6830127018922181881, 0.6830127018922202975, -0.2588190451025214056 ) ) ;
#9138=LINE ( 'NONE', #53410, #54197 ) ;
#9139=EDGE_CURVE ( 'NONE', #90720, #85257, #114255, .T. ) ;
#9140=DIRECTION ( 'NONE',  ( -0.6830127018922180770, -0.6830127018922204085, -0.2588190451025213501 ) ) ;
#9141=CARTESIAN_POINT ( 'NONE',  ( 48.29974487139158867, -27.71228299555239971, 4.000000000000000000 ) ) ;
#9143=CARTESIAN_POINT ( 'NONE',  ( -2.563198967791689764, -12.74070752338415247, 9.898150129686381860 ) ) ;
#9144=VERTEX_POINT ( 'NONE', #2622 ) ;
#9145=AXIS2_PLACEMENT_3D ( 'NONE', #140014, #16779, #18169 ) ;
#9146=FACE_OUTER_BOUND ( 'NONE', #67145, .T. ) ;
#9147=DIRECTION ( 'NONE',  ( 0.7071067811865487940, 0.7071067811865463515, 0.000000000000000000 ) ) ;
#9150=ADVANCED_FACE ( 'NONE', ( #81666 ), #3329, .F. ) ;
#9151=ORIENTED_EDGE ( 'NONE', *, *, #8038, .F. ) ;
#9152=PLANE ( 'NONE',  #34173 ) ;
#9153=ORIENTED_EDGE ( 'NONE', *, *, #14514, .F. ) ;
#9154=AXIS2_PLACEMENT_3D ( 'NONE', #92681, #39777, #115841 ) ;
#9155=ORIENTED_EDGE ( 'NONE', *, *, #62325, .F. ) ;
#9157=VECTOR ( 'NONE', #112022, 1000.000000000000000 ) ;
#9158=EDGE_LOOP ( 'NONE', ( #28849, #81274, #122965, #14637, #17212 ) ) ;
#9159=ORIENTED_EDGE ( 'NONE', *, *, #57791, .F. ) ;
#9160=DIRECTION ( 'NONE',  ( 0.7071067811865487940, -0.7071067811865463515, 0.000000000000000000 ) ) ;
#9161=EDGE_CURVE ( 'NONE', #85868, #25060, #59893, .T. ) ;
#9164=DIRECTION ( 'NONE',  ( 0.7071067811865487940, 0.7071067811865463515, -0.000000000000000000 ) ) ;
#9165=EDGE_CURVE ( 'NONE', #24914, #83531, #46186, .T. ) ;
#9166=CARTESIAN_POINT ( 'NONE',  ( 28.17183060077627488, 3.759292476615680112, 4.000000000000000000 ) ) ;
#9167=ORIENTED_EDGE ( 'NONE', *, *, #119098, .F. ) ;
#9168=FACE_OUTER_BOUND ( 'NONE', #114419, .T. ) ;
#9169=VECTOR ( 'NONE', #3885, 1000.000000000000000 ) ;
#9170=CARTESIAN_POINT ( 'NONE',  ( -5.816011393731002066, 28.73617430169783304, 5.000000000000000000 ) ) ;
#9171=EDGE_CURVE ( 'NONE', #123192, #142351, #35305, .T. ) ;
#9172=DIRECTION ( 'NONE',  ( 2.781805975412905890E-17, -0.3543493200069152693, 0.9351131265310292928 ) ) ;
#9173=LINE ( 'NONE', #31001, #135469 ) ;
#9174=ORIENTED_EDGE ( 'NONE', *, *, #31669, .F. ) ;
#9175=EDGE_CURVE ( 'NONE', #132281, #142117, #125869, .T. ) ;
#9176=CARTESIAN_POINT ( 'NONE',  ( -27.18398860626900060, 28.73617430169806042, 5.000000000000000000 ) ) ;
#9178=VERTEX_POINT ( 'NONE', #80234 ) ;
#9179=ORIENTED_EDGE ( 'NONE', *, *, #72348, .F. ) ;
#9181=ORIENTED_EDGE ( 'NONE', *, *, #66169, .T. ) ;
#9182=AXIS2_PLACEMENT_3D ( 'NONE', #112635, #4514, #80745 ) ;
#9183=CARTESIAN_POINT ( 'NONE',  ( 0.000000000000000000, 0.000000000000000000, 5.000000000000000000 ) ) ;
#9184=CARTESIAN_POINT ( 'NONE',  ( -42.18398860626899705, 28.73617430169816700, 5.000000000000000000 ) ) ;
#9185=PLANE ( 'NONE',  #11605 ) ;
#9186=EDGE_CURVE ( 'NONE', #100169, #56865, #36685, .T. ) ;
#9187=VERTEX_POINT ( 'NONE', #83812 ) ;
#9188=CARTESIAN_POINT ( 'NONE',  ( 30.18398860626900060, 28.73617430169808173, 5.000000000000000000 ) ) ;
#9189=EDGE_LOOP ( 'NONE', ( #50606, #56404, #86175, #129009 ) ) ;
#9191=CARTESIAN_POINT ( 'NONE',  ( -30.48921356237309510, -27.52281430457076894, 5.000000000000000000 ) ) ;
#9192=LINE ( 'NONE', #143323, #27464 ) ;
#9193=CARTESIAN_POINT ( 'NONE',  ( 34.42499999999998295, 2.977185695429370504, 5.000000000000000000 ) ) ;
#9195=VERTEX_POINT ( 'NONE', #63488 ) ;
#9196=VERTEX_POINT ( 'NONE', #117789 ) ;
#9198=FACE_OUTER_BOUND ( 'NONE', #74226, .T. ) ;
#9199=CARTESIAN_POINT ( 'NONE',  ( 14.99451991528749595, 28.92564299267948513, 4.000000000000000000 ) ) ;
#9200=CARTESIAN_POINT ( 'NONE',  ( 34.92499999999998295, -22.22500000000000142, 4.500000000000000888 ) ) ;
#9201=DIRECTION ( 'NONE',  ( 0.7071067811865486830, -0.7071067811865464625, -0.000000000000000000 ) ) ;
#9202=AXIS2_PLACEMENT_3D ( 'NONE', #23862, #57227, #103526 ) ;
#9203=CARTESIAN_POINT ( 'NONE',  ( 15.29974487139158867, -27.71228299555216879, 4.000000000000000000 ) ) ;
#9205=DIRECTION ( 'NONE',  ( 1.000000000000000000, 0.000000000000000000, 0.000000000000000000 ) ) ;
#9206=DIRECTION ( 'NONE',  ( -0.3543493200069162685, -0.000000000000000000, -0.9351131265310288487 ) ) ;
#9208=CARTESIAN_POINT ( 'NONE',  ( -36.48921356237310221, -27.52281430457080802, 5.000000000000000000 ) ) ;
#9210=VECTOR ( 'NONE', #139950, 1000.000000000000000 ) ;
#9211=AXIS2_PLACEMENT_3D ( 'NONE', #76878, #45674, #88453 ) ;
#9212=AXIS2_PLACEMENT_3D ( 'NONE', #134805, #56558, #24577 ) ;
#9213=LINE ( 'NONE', #11364, #105524 ) ;
#9214=ORIENTED_EDGE ( 'NONE', *, *, #36877, .T. ) ;
#9215=VECTOR ( 'NONE', #70592, 1000.000000000000000 ) ;
#9216=LINE ( 'NONE', #18690, #43666 ) ;
#9217=PLANE ( 'NONE',  #120465 ) ;
#9218=VERTEX_POINT ( 'NONE', #128019 ) ;
#9219=PLANE ( 'NONE',  #123311 ) ;
#9220=ORIENTED_EDGE ( 'NONE', *, *, #55235, .T. ) ;
#9221=CARTESIAN_POINT ( 'NONE',  ( -25.03340032343007238, 6.759292476615653023, 12.28218704918516302 ) ) ;
#9222=VERTEX_POINT ( 'NONE', #127265 ) ;
#9223=FACE_OUTER_BOUND ( 'NONE', #136753, .T. ) ;
#9227=EDGE_CURVE ( 'NONE', #53505, #65082, #72944, .T. ) ;
#9228=DIRECTION ( 'NONE',  ( 1.000000000000000000, 0.000000000000000000, 0.000000000000000000 ) ) ;
#9230=EDGE_CURVE ( 'NONE', #52329, #65412, #83065, .T. ) ;
#9231=DIRECTION ( 'NONE',  ( 0.7071067811865487940, -0.7071067811865463515, 0.000000000000000000 ) ) ;
#9232=CARTESIAN_POINT ( 'NONE',  ( -34.42500000000001137, -22.22500000000000142, 5.000000000000000000 ) ) ;
#9233=EDGE_CURVE ( 'NONE', #31173, #25152, #117093, .T. ) ;
#9234=CARTESIAN_POINT ( 'NONE',  ( 24.48921356237309510, -27.52281430457072631, 5.000000000000000000 ) ) ;
#9237=VECTOR ( 'NONE', #133939, 999.9999999999998863 ) ;
#9239=PLANE ( 'NONE',  #80221 ) ;
#9240=ADVANCED_FACE ( 'NONE', ( #27966 ), #17771, .F. ) ;
#9241=ORIENTED_EDGE ( 'NONE', *, *, #2538, .F. ) ;
#9242=ORIENTED_EDGE ( 'NONE', *, *, #78642, .T. ) ;
#9244=DIRECTION ( 'NONE',  ( -0.000000000000000000, 0.000000000000000000, 1.000000000000000000 ) ) ;
#9245=VERTEX_POINT ( 'NONE', #62046 ) ;
#9246=EDGE_CURVE ( 'NONE', #57093, #141023, #40987, .T. ) ;
#9247=VECTOR ( 'NONE', #123617, 999.9999999999998863 ) ;
#9250=DIRECTION ( 'NONE',  ( -0.7071067811865486830, -0.7071067811865464625, 0.000000000000000000 ) ) ;
#9251=PLANE ( 'NONE',  #13098 ) ;
#9252=ORIENTED_EDGE ( 'NONE', *, *, #56366, .T. ) ;
#9254=LINE ( 'NONE', #86876, #103027 ) ;
#9255=DIRECTION ( 'NONE',  ( -0.3543493200069162685, -0.000000000000000000, -0.9351131265310288487 ) ) ;
#9256=EDGE_CURVE ( 'NONE', #124198, #75105, #95355, .T. ) ;
#9258=EDGE_CURVE ( 'NONE', #30612, #106170, #38846, .T. ) ;
#9259=VECTOR ( 'NONE', #139063, 1000.000000000000114 ) ;
#9260=CARTESIAN_POINT ( 'NONE',  ( 23.99999999999982947, 10.93112307739207623, 4.000000000000000000 ) ) ;
#9261=VERTEX_POINT ( 'NONE', #128703 ) ;
#9262=DIRECTION ( 'NONE',  ( 1.000000000000000000, 0.000000000000000000, 0.000000000000000000 ) ) ;
#9263=VECTOR ( 'NONE', #113976, 1000.000000000000000 ) ;
#9264=LINE ( 'NONE', #7863, #91571 ) ;
#9265=CARTESIAN_POINT ( 'NONE',  ( -2.994519915287485734, 28.92564299267940342, 4.000000000000000000 ) ) ;
#9266=PLANE ( 'NONE',  #103451 ) ;
#9267=ADVANCED_FACE ( 'NONE', ( #93217 ), #39577, .T. ) ;
#9268=LINE ( 'NONE', #53544, #88584 ) ;
#9270=ORIENTED_EDGE ( 'NONE', *, *, #78902, .F. ) ;
#9271=ORIENTED_EDGE ( 'NONE', *, *, #26447, .F. ) ;
#9273=VECTOR ( 'NONE', #118472, 1000.000000000000000 ) ;
#9274=ORIENTED_EDGE ( 'NONE', *, *, #126637, .F. ) ;
#9276=VECTOR ( 'NONE', #102558, 1000.000000000000000 ) ;
#9277=DIRECTION ( 'NONE',  ( -0.6830127018922180770, -0.6830127018922204085, -0.2588190451025213501 ) ) ;
#9278=ORIENTED_EDGE ( 'NONE', *, *, #40746, .F. ) ;
#9279=DIRECTION ( 'NONE',  ( 0.6830127018922181881, 0.6830127018922202975, -0.2588190451025214056 ) ) ;
#9280=CARTESIAN_POINT ( 'NONE',  ( -23.99999999999982592, -10.44781430457072346, 5.000000000000000000 ) ) ;
#9282=ORIENTED_EDGE ( 'NONE', *, *, #127140, .F. ) ;
#9284=EDGE_CURVE ( 'NONE', #50102, #95024, #40301, .T. ) ;
#9287=CARTESIAN_POINT ( 'NONE',  ( 30.48921356237309510, -27.52281430457076894, 5.000000000000000000 ) ) ;
#9288=VERTEX_POINT ( 'NONE', #116404 ) ;
#9289=ORIENTED_EDGE ( 'NONE', *, *, #137726, .F. ) ;
#9290=ORIENTED_EDGE ( 'NONE', *, *, #32543, .T. ) ;
#9291=CARTESIAN_POINT ( 'NONE',  ( -18.09843580608225366, 11.25929247661560595, 10.79108189686402852 ) ) ;
#9294=AXIS2_PLACEMENT_3D ( 'NONE', #134468, #24267, #34428 ) ;
#9296=DIRECTION ( 'NONE',  ( -0.7071067811865486830, -0.7071067811865464625, 0.000000000000000000 ) ) ;
#9297=ORIENTED_EDGE ( 'NONE', *, *, #20668, .T. ) ;
#9299=CARTESIAN_POINT ( 'NONE',  ( 1.499999999999987566, 8.900465351122152313, -2.516491619111516531 ) ) ;
#9301=ORIENTED_EDGE ( 'NONE', *, *, #61687, .F. ) ;
#9302=VERTEX_POINT ( 'NONE', #85184 ) ;
#9305=VECTOR ( 'NONE', #79995, 999.9999999999998863 ) ;
#9306=LINE ( 'NONE', #29662, #37337 ) ;
#9307=LINE ( 'NONE', #109383, #79829 ) ;
#9309=CARTESIAN_POINT ( 'NONE',  ( -5.207106781186502609, -5.240707523384230626, 5.000000000000000000 ) ) ;
#9311=EDGE_CURVE ( 'NONE', #49712, #28781, #62756, .T. ) ;
#9312=CARTESIAN_POINT ( 'NONE',  ( -12.49816348513948761, -17.24070752338410628, 8.407044977365254468 ) ) ;
#9313=LINE ( 'NONE', #116697, #99275 ) ;
#9314=VECTOR ( 'NONE', #43839, 1000.000000000000000 ) ;
#9315=AXIS2_PLACEMENT_3D ( 'NONE', #114272, #14245, #70799 ) ;
#9317=( BOUNDED_CURVE ( )  B_SPLINE_CURVE ( 3, ( #11852, #56141, #978, #45263 ),
 .UNSPECIFIED., .F., .T. ) 
 B_SPLINE_CURVE_WITH_KNOTS ( ( 4, 4 ),
 ( 1.142100667999822683, 1.182775789206201411 ),
 .UNSPECIFIED. ) 
 CURVE ( )  GEOMETRIC_REPRESENTATION_ITEM ( )  RATIONAL_B_SPLINE_CURVE ( ( 1.000000000000000000, 0.9998621326283523292, 0.9998621326283523292, 1.000000000000000000 ) ) 
 REPRESENTATION_ITEM ( '' )  );
#9319=ORIENTED_EDGE ( 'NONE', *, *, #132872, .T. ) ;
#9320=VECTOR ( 'NONE', #98705, 1000.000000000000000 ) ;
#9321=LINE ( 'NONE', #75356, #69627 ) ;
#9322=VERTEX_POINT ( 'NONE', #51880 ) ;
#9324=CARTESIAN_POINT ( 'NONE',  ( 60.29974487139158867, -27.71228299555248142, 4.000000000000000000 ) ) ;
#9325=EDGE_CURVE ( 'NONE', #130843, #3304, #129407, .T. ) ;
#9326=VERTEX_POINT ( 'NONE', #71479 ) ;
#9327=DIRECTION ( 'NONE',  ( 0.7071067811865486830, -0.7071067811865464625, -0.000000000000000000 ) ) ;
#9329=CARTESIAN_POINT ( 'NONE',  ( 60.18398860626900415, 28.73617430169829490, 5.000000000000000000 ) ) ;
#9330=ORIENTED_EDGE ( 'NONE', *, *, #60016, .T. ) ;
#9332=VECTOR ( 'NONE', #6393, 1000.000000000000227 ) ;
#9333=ORIENTED_EDGE ( 'NONE', *, *, #49280, .F. ) ;
#9335=DIRECTION ( 'NONE',  ( 0.7071067811865486830, -0.7071067811865464625, -0.000000000000000000 ) ) ;
#9336=LINE ( 'NONE', #87660, #112073 ) ;
#9338=DIRECTION ( 'NONE',  ( 0.6830127018922181881, 0.6830127018922202975, -0.2588190451025214056 ) ) ;
#9339=LINE ( 'NONE', #87664, #62128 ) ;
#9340=CARTESIAN_POINT ( 'NONE',  ( 7.828169399223474656, -2.240707523384259492, 4.000000000000000000 ) ) ;
#9341=LINE ( 'NONE', #44178, #58335 ) ;
#9343=DIRECTION ( 'NONE',  ( -0.000000000000000000, -0.3543493200069152693, 0.9351131265310292928 ) ) ;
#9345=VECTOR ( 'NONE', #52997, 1000.000000000000000 ) ;
#9346=CARTESIAN_POINT ( 'NONE',  ( 5.111623618947549019, 9.759292476615607725, 17.35367589129211652 ) ) ;
#9348=EDGE_CURVE ( 'NONE', #1016, #104350, #30093, .T. ) ;
#9349=LINE ( 'NONE', #108660, #71483 ) ;
#9350=DIRECTION ( 'NONE',  ( -0.7071067811865486830, -0.7071067811865464625, -0.000000000000000000 ) ) ;
#9351=ORIENTED_EDGE ( 'NONE', *, *, #103705, .T. ) ;
#9352=VECTOR ( 'NONE', #6742, 1000.000000000000000 ) ;
#9354=VERTEX_POINT ( 'NONE', #104808 ) ;
#9355=ORIENTED_EDGE ( 'NONE', *, *, #120662, .T. ) ;
#9356=CARTESIAN_POINT ( 'NONE',  ( 3.489213562373097322, -27.52281430457057709, 5.000000000000000000 ) ) ;
#9357=ORIENTED_EDGE ( 'NONE', *, *, #20410, .T. ) ;
#9358=VECTOR ( 'NONE', #3876, 1000.000000000000000 ) ;
#9359=ORIENTED_EDGE ( 'NONE', *, *, #116154, .T. ) ;
#9360=CARTESIAN_POINT ( 'NONE',  ( 26.99999999999981171, 5.966399257802205369, 5.000000000000000000 ) ) ;
#9362=ADVANCED_FACE ( 'NONE', ( #5468 ), #93926, .F. ) ;
#9363=AXIS2_PLACEMENT_3D ( 'NONE', #16939, #40834, #138730 ) ;
#9364=EDGE_CURVE ( 'NONE', #115521, #77672, #54732, .T. ) ;
#9365=CARTESIAN_POINT ( 'NONE',  ( -36.29974487139159578, -27.71228299555231445, 4.000000000000000000 ) ) ;
#9366=ORIENTED_EDGE ( 'NONE', *, *, #82333, .T. ) ;
#9367=CARTESIAN_POINT ( 'NONE',  ( -4.499999999999968914, -14.70932175296478128, -11.46312253303836215 ) ) ;
#9368=ORIENTED_EDGE ( 'NONE', *, *, #139949, .F. ) ;
#9373=ORIENTED_EDGE ( 'NONE', *, *, #64600, .T. ) ;
#9376=DIRECTION ( 'NONE',  ( 0.7071067811865487940, -0.7071067811865463515, 0.000000000000000000 ) ) ;
#9377=DIRECTION ( 'NONE',  ( -0.000000000000000000, 0.3543493200069153248, 0.9351131265310292928 ) ) ;
#9378=ORIENTED_EDGE ( 'NONE', *, *, #76274, .F. ) ;
#9381=VECTOR ( 'NONE', #135559, 999.9999999999998863 ) ;
#9382=ORIENTED_EDGE ( 'NONE', *, *, #23556, .F. ) ;
#9384=CARTESIAN_POINT ( 'NONE',  ( -23.99999999999982947, -7.447814304570756327, 5.000000000000000000 ) ) ;
#9385=CARTESIAN_POINT ( 'NONE',  ( -34.49999999999975131, -1.912538124160733766, 4.000000000000000000 ) ) ;
#9386=FACE_OUTER_BOUND ( 'NONE', #135309, .T. ) ;
#9388=ORIENTED_EDGE ( 'NONE', *, *, #25788, .F. ) ;
#9390=LINE ( 'NONE', #108706, #72121 ) ;
#9391=CARTESIAN_POINT ( 'NONE',  ( 23.67183060077630330, -3.740707523384243505, 4.000000000000000000 ) ) ;
#9392=ORIENTED_EDGE ( 'NONE', *, *, #47642, .F. ) ;
#9393=DIRECTION ( 'NONE',  ( -1.000000000000000000, 0.000000000000000000, -0.000000000000000000 ) ) ;
#9394=VECTOR ( 'NONE', #104811, 1000.000000000000227 ) ;
#9395=FACE_OUTER_BOUND ( 'NONE', #33300, .T. ) ;
#9396=ORIENTED_EDGE ( 'NONE', *, *, #110942, .T. ) ;
#9399=ORIENTED_EDGE ( 'NONE', *, *, #43491, .F. ) ;
#9400=CARTESIAN_POINT ( 'NONE',  ( 29.99999999999979039, 1.761378380278712186, -6.096875308897186763 ) ) ;
#9401=FACE_OUTER_BOUND ( 'NONE', #17407, .T. ) ;
#9403=VERTEX_POINT ( 'NONE', #30845 ) ;
#9404=PLANE ( 'NONE',  #25713 ) ;
#9407=DIRECTION ( 'NONE',  ( 0.7071067811865487940, -0.7071067811865463515, 0.000000000000000000 ) ) ;
#9408=PLANE ( 'NONE',  #94757 ) ;
#9409=EDGE_CURVE ( 'NONE', #65559, #126328, #31542, .T. ) ;
#9411=PLANE ( 'NONE',  #109181 ) ;
#9412=DIRECTION ( 'NONE',  ( 0.7071067811865486830, -0.7071067811865464625, -0.000000000000000000 ) ) ;
#9414=DIRECTION ( 'NONE',  ( -0.7071067811865486830, -0.7071067811865464625, 0.000000000000000000 ) ) ;
#9415=CARTESIAN_POINT ( 'NONE',  ( 8.292893218813405909, -0.7407075233842735917, 5.000000000000000000 ) ) ;
#9416=CARTESIAN_POINT ( 'NONE',  ( -51.48921356237309510, -27.52281430457091460, 5.000000000000000000 ) ) ;
#9417=VECTOR ( 'NONE', #43169, 1000.000000000000000 ) ;
#9418=LINE ( 'NONE', #52939, #37246 ) ;
#9419=PLANE ( 'NONE',  #105614 ) ;
#9420=ADVANCED_FACE ( 'NONE', ( #301 ), #132311, .F. ) ;
#9421=EDGE_LOOP ( 'NONE', ( #80099, #35495, #41797, #99407, #16065, #21186 ) ) ;
#9422=EDGE_CURVE ( 'NONE', #79985, #38905, #88064, .T. ) ;
#9423=ORIENTED_EDGE ( 'NONE', *, *, #128350, .F. ) ;
#9424=ORIENTED_EDGE ( 'NONE', *, *, #52468, .F. ) ;
#9425=AXIS2_PLACEMENT_3D ( 'NONE', #35276, #65774, #109937 ) ;
#9427=VERTEX_POINT ( 'NONE', #98230 ) ;
#9428=VERTEX_POINT ( 'NONE', #75769 ) ;
#9430=LINE ( 'NONE', #8701, #87279 ) ;
#9432=VECTOR ( 'NONE', #67591, 999.9999999999998863 ) ;
#9433=AXIS2_PLACEMENT_3D ( 'NONE', #127126, #27826, #72091 ) ;
#9434=VECTOR ( 'NONE', #109097, 1000.000000000000000 ) ;
#9436=VERTEX_POINT ( 'NONE', #109808 ) ;
#9437=DIRECTION ( 'NONE',  ( -0.7071067811865486830, -0.7071067811865464625, 0.000000000000000000 ) ) ;
#9439=CARTESIAN_POINT ( 'NONE',  ( -3.328169399223502189, -0.7407075233842770334, 4.000000000000000000 ) ) ;
#9440=EDGE_CURVE ( 'NONE', #104604, #138539, #122095, .T. ) ;
#9441=DIRECTION ( 'NONE',  ( -0.6830127018922181881, 0.6830127018922202975, -0.2588190451025214056 ) ) ;
#9442=CARTESIAN_POINT ( 'NONE',  ( 0.000000000000000000, 20.70535890316561023, 1.956823837851916714 ) ) ;
#9444=EDGE_CURVE ( 'NONE', #10446, #109601, #53269, .T. ) ;
#9446=DIRECTION ( 'NONE',  ( 0.6830127018922180770, -0.6830127018922204085, -0.2588190451025213501 ) ) ;
#9447=VECTOR ( 'NONE', #107720, 1000.000000000000000 ) ;
#9448=CARTESIAN_POINT ( 'NONE',  ( -18.18398860626898994, 28.73617430169800002, 5.000000000000000000 ) ) ;
#9452=EDGE_CURVE ( 'NONE', #66483, #118907, #119933, .T. ) ;
#9453=LINE ( 'NONE', #87057, #23576 ) ;
#9454=VERTEX_POINT ( 'NONE', #77215 ) ;
#9455=ORIENTED_EDGE ( 'NONE', *, *, #10680, .F. ) ;
#9458=VECTOR ( 'NONE', #42900, 999.9999999999998863 ) ;
#9459=CARTESIAN_POINT ( 'NONE',  ( 5.816011393731002066, 28.73617430169783304, 5.000000000000000000 ) ) ;
#9461=CYLINDRICAL_SURFACE ( 'NONE', #57184, 0.5000000000000004441 ) ;
#9462=EDGE_CURVE ( 'NONE', #139894, #135322, #130152, .T. ) ;
#9463=PLANE ( 'NONE',  #124369 ) ;
#9465=DIRECTION ( 'NONE',  ( 0.7071067811865487940, 0.7071067811865463515, -0.000000000000000000 ) ) ;
#9466=DIRECTION ( 'NONE',  ( -0.7071067811865486830, -0.7071067811865464625, 0.000000000000000000 ) ) ;
#9467=AXIS2_PLACEMENT_3D ( 'NONE', #64097, #60009, #104172 ) ;
#9468=VECTOR ( 'NONE', #96304, 1000.000000000000000 ) ;
#9470=ORIENTED_EDGE ( 'NONE', *, *, #91636, .T. ) ;
#9471=VECTOR ( 'NONE', #44749, 1000.000000000000000 ) ;
#9472=ORIENTED_EDGE ( 'NONE', *, *, #27720, .F. ) ;
#9473=EDGE_CURVE ( 'NONE', #108316, #104393, #76491, .T. ) ;
#9474=FACE_OUTER_BOUND ( 'NONE', #118525, .T. ) ;
#9475=AXIS2_PLACEMENT_3D ( 'NONE', #55295, #45159, #121937 ) ;
#9476=CARTESIAN_POINT ( 'NONE',  ( -12.79289321881336150, 0.7592924766157052030, 5.000000000000000000 ) ) ;
#9477=CARTESIAN_POINT ( 'NONE',  ( 2.994519915287485734, 28.92564299267940342, 4.000000000000000000 ) ) ;
#9479=ORIENTED_EDGE ( 'NONE', *, *, #20367, .T. ) ;
#9482=AXIS2_PLACEMENT_3D ( 'NONE', #78294, #90597, #89857 ) ;
#9483=CARTESIAN_POINT ( 'NONE',  ( 33.29974487139158867, -27.71228299555229313, 4.000000000000000000 ) ) ;
#9484=DIRECTION ( 'NONE',  ( -0.3543493200069163240, -0.000000000000000000, -0.9351131265310288487 ) ) ;
#9485=CARTESIAN_POINT ( 'NONE',  ( 24.48921356237309510, -27.52281430457072631, 5.000000000000000000 ) ) ;
#9486=EDGE_CURVE ( 'NONE', #63259, #71467, #107654, .T. ) ;
#9487=ADVANCED_FACE ( 'NONE', ( #121387 ), #142454, .T. ) ;
#9488=VECTOR ( 'NONE', #28079, 1000.000000000000227 ) ;
#9490=ORIENTED_EDGE ( 'NONE', *, *, #130933, .T. ) ;
#9491=DIRECTION ( 'NONE',  ( 0.7071067811865486830, -0.7071067811865464625, -0.000000000000000000 ) ) ;
#9492=EDGE_LOOP ( 'NONE', ( #131528, #32597, #58872, #136148 ) ) ;
#9493=ORIENTED_EDGE ( 'NONE', *, *, #81334, .T. ) ;
#9495=EDGE_LOOP ( 'NONE', ( #115487, #33363, #508, #26146 ) ) ;
#9498=ORIENTED_EDGE ( 'NONE', *, *, #25668, .F. ) ;
#9499=CARTESIAN_POINT ( 'NONE',  ( -34.42500000000001137, 5.977185695429358958, 5.000000000000000000 ) ) ;
#9500=ADVANCED_FACE ( 'NONE', ( #52563 ), #22755, .F. ) ;
#9501=DIRECTION ( 'NONE',  ( -0.6830127018922181881, 0.6830127018922202975, -0.2588190451025214056 ) ) ;
#9503=CARTESIAN_POINT ( 'NONE',  ( 16.49999999999989342, 16.46639925780208813, 5.000000000000000000 ) ) ;
#9504=DIRECTION ( 'NONE',  ( -0.6830127018922180770, -0.6830127018922204085, -0.2588190451025213501 ) ) ;
#9505=FACE_BOUND ( 'NONE', #45247, .T. ) ;
#9506=EDGE_LOOP ( 'NONE', ( #34029, #127191, #118906, #25606 ) ) ;
#9507=CARTESIAN_POINT ( 'NONE',  ( -1.499999999999989120, -13.91253812416061564, 4.000000000000000000 ) ) ;
#9508=EDGE_CURVE ( 'NONE', #116772, #128234, #110493, .T. ) ;
#9509=DIRECTION ( 'NONE',  ( -0.7071067811865486830, 0.7071067811865464625, 0.000000000000000000 ) ) ;
#9510=CARTESIAN_POINT ( 'NONE',  ( 17.70025512860841488, -27.71228299555193786, 4.000000000000000000 ) ) ;
#9511=ORIENTED_EDGE ( 'NONE', *, *, #29386, .F. ) ;
#9513=ORIENTED_EDGE ( 'NONE', *, *, #116309, .T. ) ;
#9514=VERTEX_POINT ( 'NONE', #109078 ) ;
#9515=AXIS2_PLACEMENT_3D ( 'NONE', #40004, #107359, #96448 ) ;
#9516=CARTESIAN_POINT ( 'NONE',  ( 19.05000000000000071, 3.174999999999997158, 0.000000000000000000 ) ) ;
#9517=( BOUNDED_CURVE ( )  B_SPLINE_CURVE ( 3, ( #123115, #134719, #113635, #81770 ),
 .UNSPECIFIED., .F., .F. ) 
 B_SPLINE_CURVE_WITH_KNOTS ( ( 4, 4 ),
 ( 4.874499669516390910, 4.920172610314182293 ),
 .UNSPECIFIED. ) 
 CURVE ( )  GEOMETRIC_REPRESENTATION_ITEM ( )  RATIONAL_B_SPLINE_CURVE ( ( 1.000000000000000000, 0.9998261727610758820, 0.9998261727610758820, 1.000000000000000000 ) ) 
 REPRESENTATION_ITEM ( '' )  );
#9520=EDGE_LOOP ( 'NONE', ( #84992, #119631, #79342, #10026 ) ) ;
#9521=FACE_OUTER_BOUND ( 'NONE', #73903, .T. ) ;
#9522=ORIENTED_EDGE ( 'NONE', *, *, #20555, .T. ) ;
#9524=ORIENTED_EDGE ( 'NONE', *, *, #13878, .F. ) ;
#9525=EDGE_CURVE ( 'NONE', #89076, #84967, #9773, .T. ) ;
#9526=LINE ( 'NONE', #63272, #132493 ) ;
#9527=VECTOR ( 'NONE', #57402, 1000.000000000000000 ) ;
#9528=VECTOR ( 'NONE', #84479, 1000.000000000000227 ) ;
#9529=VECTOR ( 'NONE', #87462, 1000.000000000000000 ) ;
#9530=CARTESIAN_POINT ( 'NONE',  ( -21.18398860626899349, 28.73617430169802134, 5.000000000000000000 ) ) ;
#9533=PLANE ( 'NONE',  #108476 ) ;
#9534=DIRECTION ( 'NONE',  ( 0.6830127018922181881, 0.6830127018922202975, -0.2588190451025214056 ) ) ;
#9535=DIRECTION ( 'NONE',  ( -0.7071067811865486830, -0.7071067811865464625, 0.000000000000000000 ) ) ;
#9536=EDGE_LOOP ( 'NONE', ( #3452, #82198, #55651, #6315 ) ) ;
#9537=VECTOR ( 'NONE', #139264, 999.9999999999998863 ) ;
#9538=VECTOR ( 'NONE', #128237, 1000.000000000000000 ) ;
#9540=VECTOR ( 'NONE', #15816, 1000.000000000000000 ) ;
#9542=CARTESIAN_POINT ( 'NONE',  ( -13.49999999999990052, -19.91253812416055524, 4.000000000000000000 ) ) ;
#9543=DIRECTION ( 'NONE',  ( 0.7071067811865486830, -0.7071067811865464625, -0.000000000000000000 ) ) ;
#9545=VECTOR ( 'NONE', #831, 999.9999999999998863 ) ;
#9546=ORIENTED_EDGE ( 'NONE', *, *, #141244, .F. ) ;
#9547=LINE ( 'NONE', #8119, #99947 ) ;
#9549=EDGE_CURVE ( 'NONE', #17021, #49295, #136544, .T. ) ;
#9550=EDGE_CURVE ( 'NONE', #106128, #44075, #79376, .T. ) ;
#9551=DIRECTION ( 'NONE',  ( 0.7071067811865486830, -0.7071067811865464625, -0.000000000000000000 ) ) ;
#9552=ORIENTED_EDGE ( 'NONE', *, *, #9175, .T. ) ;
#9553=VECTOR ( 'NONE', #140886, 1000.000000000000227 ) ;
#9554=CARTESIAN_POINT ( 'NONE',  ( 7.828169399223474656, -20.24070752338407431, 4.000000000000000000 ) ) ;
#9555=LINE ( 'NONE', #10282, #102305 ) ;
#9557=LINE ( 'NONE', #53830, #141043 ) ;
#9558=ORIENTED_EDGE ( 'NONE', *, *, #63356, .T. ) ;
#9560=EDGE_CURVE ( 'NONE', #6090, #23067, #112662, .T. ) ;
#9562=DIRECTION ( 'NONE',  ( -0.3543493200069163240, -0.000000000000000000, 0.9351131265310288487 ) ) ;
#9563=CARTESIAN_POINT ( 'NONE',  ( -3.183988606268992161, 28.73617430169789699, 5.000000000000000000 ) ) ;
#9564=CARTESIAN_POINT ( 'NONE',  ( -69.18398860626899705, 28.73617430169835529, 5.000000000000000000 ) ) ;
#9567=EDGE_LOOP ( 'NONE', ( #80120, #35216, #91779, #80750 ) ) ;
#9569=CARTESIAN_POINT ( 'NONE',  ( 0.000000000000000000, 0.000000000000000000, 5.000000000000000000 ) ) ;
#9571=EDGE_CURVE ( 'NONE', #65516, #65242, #122829, .T. ) ;
#9574=VECTOR ( 'NONE', #77318, 1000.000000000000227 ) ;
#9575=VECTOR ( 'NONE', #53821, 1000.000000000000000 ) ;
#9576=DIRECTION ( 'NONE',  ( 0.7071067811865487940, -0.7071067811865463515, 0.000000000000000000 ) ) ;
#9578=ORIENTED_EDGE ( 'NONE', *, *, #13778, .T. ) ;
#9579=EDGE_CURVE ( 'NONE', #40143, #133726, #92316, .T. ) ;
#9580=FACE_OUTER_BOUND ( 'NONE', #28645, .T. ) ;
#9581=VECTOR ( 'NONE', #81723, 1000.000000000000000 ) ;
#9582=CARTESIAN_POINT ( 'NONE',  ( -3.792893218813429446, 18.75929247661552779, 5.000000000000000000 ) ) ;
#9584=DIRECTION ( 'NONE',  ( -0.3543493200069162685, -0.000000000000000000, -0.9351131265310288487 ) ) ;
#9585=CARTESIAN_POINT ( 'NONE',  ( 6.299744871391586898, -27.71228299555210484, 4.000000000000000000 ) ) ;
#9586=ORIENTED_EDGE ( 'NONE', *, *, #55998, .T. ) ;
#9589=CARTESIAN_POINT ( 'NONE',  ( 3.489213562373097322, -27.52281430457057709, 5.000000000000000000 ) ) ;
#9590=DIRECTION ( 'NONE',  ( 0.6830127018922180770, -0.6830127018922204085, -0.2588190451025213501 ) ) ;
#9591=DIRECTION ( 'NONE',  ( -0.000000000000000000, 0.3543493200069153248, 0.9351131265310292928 ) ) ;
#9592=FACE_OUTER_BOUND ( 'NONE', #117514, .T. ) ;
#9593=ORIENTED_EDGE ( 'NONE', *, *, #34526, .T. ) ;
#9594=EDGE_CURVE ( 'NONE', #126646, #20150, #11904, .T. ) ;
#9595=CARTESIAN_POINT ( 'NONE',  ( 19.05000000000000071, 3.174999999999997158, 5.000000000000000000 ) ) ;
#9596=LINE ( 'NONE', #53872, #113831 ) ;
#9597=VECTOR ( 'NONE', #131284, 1000.000000000000227 ) ;
#9598=FACE_OUTER_BOUND ( 'NONE', #28762, .T. ) ;
#9599=VECTOR ( 'NONE', #114633, 1000.000000000000000 ) ;
#9600=CARTESIAN_POINT ( 'NONE',  ( 42.18398860626899705, 28.73617430169816700, 5.000000000000000000 ) ) ;
#9602=PLANE ( 'NONE',  #141338 ) ;
#9603=EDGE_CURVE ( 'NONE', #114032, #121130, #100374, .T. ) ;
#9604=EDGE_CURVE ( 'NONE', #114250, #5707, #67783, .T. ) ;
#9605=ORIENTED_EDGE ( 'NONE', *, *, #18051, .T. ) ;
#9606=VERTEX_POINT ( 'NONE', #90190 ) ;
#9607=DIRECTION ( 'NONE',  ( 0.7071067811865487940, -0.7071067811865463515, 0.000000000000000000 ) ) ;
#9608=ORIENTED_EDGE ( 'NONE', *, *, #21387, .F. ) ;
#9609=ORIENTED_EDGE ( 'NONE', *, *, #15540, .T. ) ;
#9610=VECTOR ( 'NONE', #92866, 1000.000000000000000 ) ;
#9612=CARTESIAN_POINT ( 'NONE',  ( -34.92500000000001137, 22.22500000000000142, 4.000000000000000000 ) ) ;
#9614=ORIENTED_EDGE ( 'NONE', *, *, #139692, .T. ) ;
#9616=CARTESIAN_POINT ( 'NONE',  ( 30.18398860626900060, 28.73617430169808173, 5.000000000000000000 ) ) ;
#9617=FACE_OUTER_BOUND ( 'NONE', #119504, .T. ) ;
#9618=EDGE_CURVE ( 'NONE', #102027, #57345, #91629, .T. ) ;
#9619=FACE_OUTER_BOUND ( 'NONE', #45078, .T. ) ;
#9620=DIRECTION ( 'NONE',  ( 0.6830127018922180770, -0.6830127018922204085, -0.2588190451025213501 ) ) ;
#9622=EDGE_CURVE ( 'NONE', #139467, #70462, #14777, .T. ) ;
#9623=CARTESIAN_POINT ( 'NONE',  ( 30.61838490601977725, -2.240707523384260824, 13.37739548510232268 ) ) ;
#9624=DIRECTION ( 'NONE',  ( 0.7071067811865487940, 0.7071067811865463515, -0.000000000000000000 ) ) ;
#9626=AXIS2_PLACEMENT_3D ( 'NONE', #30512, #75444, #121066 ) ;
#9627=CARTESIAN_POINT ( 'NONE',  ( -10.49999999999992184, 16.46639925780209524, 5.000000000000000000 ) ) ;
#9628=DIRECTION ( 'NONE',  ( -0.000000000000000000, 0.000000000000000000, 1.000000000000000000 ) ) ;
#9630=LINE ( 'NONE', #11771, #117574 ) ;
#9632=EDGE_CURVE ( 'NONE', #25081, #14507, #69922, .T. ) ;
#9633=CARTESIAN_POINT ( 'NONE',  ( -9.489213562373095101, -27.52281430457062328, 5.000000000000000000 ) ) ;
#9634=EDGE_LOOP ( 'NONE', ( #92215, #32995, #139085, #62177 ) ) ;
#9635=ORIENTED_EDGE ( 'NONE', *, *, #79584, .T. ) ;
#9637=ADVANCED_FACE ( 'NONE', ( #46756 ), #36532, .T. ) ;
#9638=CARTESIAN_POINT ( 'NONE',  ( 21.79614956108759216, 8.475608720613170277, 4.664130618528504080 ) ) ;
#9639=FACE_OUTER_BOUND ( 'NONE', #140004, .T. ) ;
#9640=CARTESIAN_POINT ( 'NONE',  ( -54.48921356237310221, -27.52281430457093236, 5.000000000000000000 ) ) ;
#9641=VERTEX_POINT ( 'NONE', #3852 ) ;
#9643=EDGE_CURVE ( 'NONE', #95326, #25399, #101058, .T. ) ;
#9644=VECTOR ( 'NONE', #75393, 1000.000000000000227 ) ;
#9645=DIRECTION ( 'NONE',  ( -0.000000000000000000, 0.3543493200069153248, 0.9351131265310292928 ) ) ;
#9646=DIRECTION ( 'NONE',  ( 1.000000000000000000, 0.000000000000000000, 0.000000000000000000 ) ) ;
#9647=AXIS2_PLACEMENT_3D ( 'NONE', #125297, #25987, #50590 ) ;
#9650=ORIENTED_EDGE ( 'NONE', *, *, #68813, .F. ) ;
#9651=ORIENTED_EDGE ( 'NONE', *, *, #95559, .F. ) ;
#9652=VECTOR ( 'NONE', #10656, 1000.000000000000000 ) ;
#9653=ORIENTED_EDGE ( 'NONE', *, *, #138983, .T. ) ;
#9654=VECTOR ( 'NONE', #11392, 1000.000000000000000 ) ;
#9655=EDGE_CURVE ( 'NONE', #94256, #112217, #1714, .T. ) ;
#9658=DIRECTION ( 'NONE',  ( 0.6830127018922181881, 0.6830127018922202975, -0.2588190451025214056 ) ) ;
#9659=VECTOR ( 'NONE', #140023, 1000.000000000000000 ) ;
#9660=AXIS2_PLACEMENT_3D ( 'NONE', #97862, #8654, #9376 ) ;
#9661=DIRECTION ( 'NONE',  ( -0.3543493200069162685, -0.000000000000000000, -0.9351131265310288487 ) ) ;
#9663=CARTESIAN_POINT ( 'NONE',  ( -2.999999999999971578, 10.55218569542906337, 5.000000000000000000 ) ) ;
#9664=EDGE_LOOP ( 'NONE', ( #141310, #4968, #33670 ) ) ;
#9665=DIRECTION ( 'NONE',  ( 0.7071067811865486830, -0.7071067811865464625, -0.000000000000000000 ) ) ;
#9667=ORIENTED_EDGE ( 'NONE', *, *, #134730, .F. ) ;
#9669=CARTESIAN_POINT ( 'NONE',  ( -9.489213562373095101, -27.52281430457062328, 5.000000000000000000 ) ) ;
#9670=DIRECTION ( 'NONE',  ( -0.000000000000000000, -0.3543493200069152693, 0.9351131265310292928 ) ) ;
#9671=LINE ( 'NONE', #43052, #65451 ) ;
#9673=EDGE_CURVE ( 'NONE', #121898, #69514, #133715, .T. ) ;
#9674=CARTESIAN_POINT ( 'NONE',  ( -20.99451991528748707, 28.92564299267952777, 4.000000000000000000 ) ) ;
#9675=CARTESIAN_POINT ( 'NONE',  ( 25.17183060077630330, -14.24070752338413293, 4.000000000000000000 ) ) ;
#9676=EDGE_CURVE ( 'NONE', #112076, #63804, #111213, .T. ) ;
#9680=FACE_OUTER_BOUND ( 'NONE', #24240, .T. ) ;
#9681=DIRECTION ( 'NONE',  ( 0.7071067811865487940, 0.7071067811865463515, -0.000000000000000000 ) ) ;
#9682=FACE_OUTER_BOUND ( 'NONE', #16125, .T. ) ;
#9685=CARTESIAN_POINT ( 'NONE',  ( 3.489213562373097322, -27.52281430457057709, 5.000000000000000000 ) ) ;
#9686=FACE_OUTER_BOUND ( 'NONE', #9810, .T. ) ;
#9687=EDGE_CURVE ( 'NONE', #140721, #129923, #56895, .T. ) ;
#9688=ORIENTED_EDGE ( 'NONE', *, *, #71799, .T. ) ;
#9689=VECTOR ( 'NONE', #67157, 1000.000000000000114 ) ;
#9691=AXIS2_PLACEMENT_3D ( 'NONE', #214, #44519, #88719 ) ;
#9692=DIRECTION ( 'NONE',  ( -0.7071067811865486830, 0.7071067811865464625, 0.000000000000000000 ) ) ;
#9694=VECTOR ( 'NONE', #108675, 1000.000000000000000 ) ;
#9695=CARTESIAN_POINT ( 'NONE',  ( 24.18398860626899705, 28.73617430169804265, 5.000000000000000000 ) ) ;
#9696=CARTESIAN_POINT ( 'NONE',  ( -42.18398860626899705, 28.73617430169816700, 5.000000000000000000 ) ) ;
#9697=VECTOR ( 'NONE', #123456, 1000.000000000000000 ) ;
#9698=CARTESIAN_POINT ( 'NONE',  ( 12.04658813629536773, 14.25929247661557042, 18.84478104361324924 ) ) ;
#9699=FACE_BOUND ( 'NONE', #92046, .T. ) ;
#9701=DIRECTION ( 'NONE',  ( 0.6830127018922180770, -0.6830127018922204085, -0.2588190451025213501 ) ) ;
#9702=CARTESIAN_POINT ( 'NONE',  ( -14.99999999999988809, -8.151047557385080466, -8.977947279169763206 ) ) ;
#9703=PLANE ( 'NONE',  #59798 ) ;
#9704=ORIENTED_EDGE ( 'NONE', *, *, #102063, .T. ) ;
#9705=VECTOR ( 'NONE', #140945, 1000.000000000000000 ) ;
#9706=CARTESIAN_POINT ( 'NONE',  ( 14.99451991528749595, 28.92564299267948513, 4.000000000000000000 ) ) ;
#9708=ORIENTED_EDGE ( 'NONE', *, *, #138313, .T. ) ;
#9710=EDGE_LOOP ( 'NONE', ( #127931, #33466, #59497, #55446 ) ) ;
#9711=CARTESIAN_POINT ( 'NONE',  ( 0.000000000000000000, 0.000000000000000000, 5.000000000000000000 ) ) ;
#9713=ADVANCED_FACE ( 'NONE', ( #101784 ), #85023, .F. ) ;
#9714=ORIENTED_EDGE ( 'NONE', *, *, #133090, .T. ) ;
#9715=DIRECTION ( 'NONE',  ( 0.7071067811865487940, 0.7071067811865463515, 0.000000000000000000 ) ) ;
#9717=PLANE ( 'NONE',  #42553 ) ;
#9718=CARTESIAN_POINT ( 'NONE',  ( 0.000000000000000000, 0.000000000000000000, 5.000000000000000000 ) ) ;
#9720=DIRECTION ( 'NONE',  ( -0.000000000000000000, 0.3543493200069153248, 0.9351131265310292928 ) ) ;
#9723=ORIENTED_EDGE ( 'NONE', *, *, #39513, .T. ) ;
#9724=VECTOR ( 'NONE', #37976, 1000.000000000000000 ) ;
#9725=LINE ( 'NONE', #43105, #14464 ) ;
#9726=ORIENTED_EDGE ( 'NONE', *, *, #53000, .T. ) ;
#9728=CARTESIAN_POINT ( 'NONE',  ( 24.48921356237309510, -27.52281430457072631, 5.000000000000000000 ) ) ;
#9729=EDGE_CURVE ( 'NONE', #98816, #96665, #140146, .T. ) ;
#9732=ADVANCED_FACE ( 'NONE', ( #137288 ), #5305, .F. ) ;
#9733=ORIENTED_EDGE ( 'NONE', *, *, #35243, .T. ) ;
#9735=ORIENTED_EDGE ( 'NONE', *, *, #66766, .F. ) ;
#9736=LINE ( 'NONE', #27375, #57485 ) ;
#9737=EDGE_CURVE ( 'NONE', #129536, #76705, #29980, .T. ) ;
#9742=EDGE_LOOP ( 'NONE', ( #129045, #64031, #2471, #14722 ) ) ;
#9744=FACE_OUTER_BOUND ( 'NONE', #42705, .T. ) ;
#9745=ORIENTED_EDGE ( 'NONE', *, *, #129908, .F. ) ;
#9746=DIRECTION ( 'NONE',  ( 0.6830127018922180770, -0.6830127018922204085, -0.2588190451025213501 ) ) ;
#9748=AXIS2_PLACEMENT_3D ( 'NONE', #112996, #34749, #15099 ) ;
#9749=DIRECTION ( 'NONE',  ( -0.7071067811865487940, 0.7071067811865463515, -0.000000000000000000 ) ) ;
#9751=AXIS2_PLACEMENT_3D ( 'NONE', #110936, #78351, #121821 ) ;
#9752=VERTEX_POINT ( 'NONE', #27795 ) ;
#9753=DIRECTION ( 'NONE',  ( -0.7071067811865487940, 0.7071067811865463515, -0.000000000000000000 ) ) ;
#9755=LINE ( 'NONE', #42429, #49223 ) ;
#9756=AXIS2_PLACEMENT_3D ( 'NONE', #22554, #77702, #66816 ) ;
#9757=CARTESIAN_POINT ( 'NONE',  ( -22.49999999999984013, 9.052185695429074030, 5.000000000000000000 ) ) ;
#9758=EDGE_CURVE ( 'NONE', #33217, #100010, #138718, .T. ) ;
#9759=VECTOR ( 'NONE', #24527, 999.9999999999998863 ) ;
#9760=ORIENTED_EDGE ( 'NONE', *, *, #60978, .T. ) ;
#9762=ORIENTED_EDGE ( 'NONE', *, *, #41366, .F. ) ;
#9763=ORIENTED_EDGE ( 'NONE', *, *, #88313, .T. ) ;
#9764=VERTEX_POINT ( 'NONE', #72060 ) ;
#9765=CARTESIAN_POINT ( 'NONE',  ( -34.49999999999976552, 18.43112307739199451, 4.000000000000000000 ) ) ;
#9766=DIRECTION ( 'NONE',  ( 1.000000000000000000, 0.000000000000000000, 0.000000000000000000 ) ) ;
#9767=VECTOR ( 'NONE', #114992, 1000.000000000000000 ) ;
#9768=VECTOR ( 'NONE', #127888, 1000.000000000000000 ) ;
#9769=AXIS2_PLACEMENT_3D ( 'NONE', #114862, #137378, #38069 ) ;
#9770=ADVANCED_FACE ( 'NONE', ( #61197 ), #40821, .F. ) ;
#9771=DIRECTION ( 'NONE',  ( -0.000000000000000000, -0.000000000000000000, 1.000000000000000000 ) ) ;
#9772=CARTESIAN_POINT ( 'NONE',  ( -3.707106781186508826, -15.74070752338412049, 5.000000000000000000 ) ) ;
#9773=LINE ( 'NONE', #88794, #65938 ) ;
#9774=DIRECTION ( 'NONE',  ( 0.6830127018922181881, 0.6830127018922202975, -0.2588190451025214056 ) ) ;
#9775=VERTEX_POINT ( 'NONE', #70634 ) ;
#9777=VERTEX_POINT ( 'NONE', #103900 ) ;
#9778=EDGE_CURVE ( 'NONE', #27605, #111099, #7444, .T. ) ;
#9779=CARTESIAN_POINT ( 'NONE',  ( -28.41009064519814942, 9.759292476615618384, 11.28811694763772344 ) ) ;
#9780=CARTESIAN_POINT ( 'NONE',  ( -15.32816939922341959, -12.74070752338415247, 4.000000000000000000 ) ) ;
#9781=ORIENTED_EDGE ( 'NONE', *, *, #48078, .F. ) ;
#9782=CARTESIAN_POINT ( 'NONE',  ( 14.67183060077636370, -18.74070752338408852, 4.000000000000000000 ) ) ;
#9783=CARTESIAN_POINT ( 'NONE',  ( 0.4733609636421477473, -5.240707523384232402, 16.25846745537495863 ) ) ;
#9784=ORIENTED_EDGE ( 'NONE', *, *, #25315, .T. ) ;
#9785=ORIENTED_EDGE ( 'NONE', *, *, #41397, .T. ) ;
#9787=CARTESIAN_POINT ( 'NONE',  ( -4.828169399223491531, 9.759292476615618384, 4.000000000000000000 ) ) ;
#9788=LINE ( 'NONE', #120677, #32674 ) ;
#9789=CARTESIAN_POINT ( 'NONE',  ( -32.29289321881322650, 14.25929247661557042, 5.000000000000000000 ) ) ;
#9790=CARTESIAN_POINT ( 'NONE',  ( -34.75611968250419892, -21.18706574529240783, 4.955485411084905145 ) ) ;
#9792=VECTOR ( 'NONE', #108298, 1000.000000000000000 ) ;
#9793=LINE ( 'NONE', #96764, #90433 ) ;
#9794=ADVANCED_FACE ( 'NONE', ( #27073 ), #50276, .T. ) ;
#9795=EDGE_CURVE ( 'NONE', #17066, #104226, #117621, .T. ) ;
#9797=DIRECTION ( 'NONE',  ( -0.7071067811865487940, 0.7071067811865463515, -0.000000000000000000 ) ) ;
#9799=VECTOR ( 'NONE', #42609, 999.9999999999998863 ) ;
#9800=EDGE_LOOP ( 'NONE', ( #81298, #61337, #51087, #4171 ) ) ;
#9801=DIRECTION ( 'NONE',  ( 0.000000000000000000, 0.000000000000000000, -1.000000000000000000 ) ) ;
#9802=EDGE_LOOP ( 'NONE', ( #71288, #6805, #110044, #32127 ) ) ;
#9803=CARTESIAN_POINT ( 'NONE',  ( -26.99999999999980815, -15.41253812416059432, 4.000000000000000000 ) ) ;
#9806=ORIENTED_EDGE ( 'NONE', *, *, #77823, .T. ) ;
#9807=EDGE_CURVE ( 'NONE', #44162, #79780, #115475, .T. ) ;
#9808=FACE_OUTER_BOUND ( 'NONE', #27780, .T. ) ;
#9809=CARTESIAN_POINT ( 'NONE',  ( 21.48921356237309155, -27.52281430457070499, 5.000000000000000000 ) ) ;
#9810=EDGE_LOOP ( 'NONE', ( #88364, #3939, #102750, #23216 ) ) ;
#9811=DIRECTION ( 'NONE',  ( 0.6830127018922180770, -0.6830127018922204085, -0.2588190451025213501 ) ) ;
#9812=ADVANCED_FACE ( 'NONE', ( #94466 ), #39406, .F. ) ;
#9813=DIRECTION ( 'NONE',  ( 0.7071067811865487940, -0.7071067811865463515, 0.000000000000000000 ) ) ;
#9814=CARTESIAN_POINT ( 'NONE',  ( -39.48921356237310221, -27.52281430457082934, 5.000000000000000000 ) ) ;
#9815=VERTEX_POINT ( 'NONE', #17609 ) ;
#9816=ORIENTED_EDGE ( 'NONE', *, *, #38312, .T. ) ;
#9817=DIRECTION ( 'NONE',  ( -0.7071067811865486830, -0.7071067811865464625, -0.000000000000000000 ) ) ;
#9818=CARTESIAN_POINT ( 'NONE',  ( -16.49999999999988276, -10.53360074219763121, 5.000000000000000000 ) ) ;
#9819=LINE ( 'NONE', #134478, #100661 ) ;
#9820=DIRECTION ( 'NONE',  ( -0.6830127018922181881, 0.6830127018922202975, -0.2588190451025214056 ) ) ;
#9822=CARTESIAN_POINT ( 'NONE',  ( 11.29387692260795717, 22.22500000000000142, 4.000000000000000000 ) ) ;
#9823=LINE ( 'NONE', #120719, #46070 ) ;
#9824=ORIENTED_EDGE ( 'NONE', *, *, #140884, .F. ) ;
#9826=EDGE_CURVE ( 'NONE', #49111, #97582, #128546, .T. ) ;
#9827=DIRECTION ( 'NONE',  ( -0.7071067811865486830, -0.7071067811865464625, 0.000000000000000000 ) ) ;
#9828=CARTESIAN_POINT ( 'NONE',  ( 24.78162688292477256, 21.74787736706806385, 4.999607392498049308 ) ) ;
#9830=VECTOR ( 'NONE', #64262, 999.9999999999998863 ) ;
#9831=AXIS2_PLACEMENT_3D ( 'NONE', #72289, #49079, #104113 ) ;
#9832=ORIENTED_EDGE ( 'NONE', *, *, #41753, .T. ) ;
#9833=EDGE_CURVE ( 'NONE', #74099, #59626, #18308, .T. ) ;
#9834=LINE ( 'NONE', #54794, #111608 ) ;
#9835=ORIENTED_EDGE ( 'NONE', *, *, #58100, .F. ) ;
#9838=DIRECTION ( 'NONE',  ( 0.7071067811865486830, -0.7071067811865464625, -0.000000000000000000 ) ) ;
#9839=ORIENTED_EDGE ( 'NONE', *, *, #61997, .T. ) ;
#9841=CARTESIAN_POINT ( 'NONE',  ( -22.49999999999984723, 11.52377502935400955, -1.522421517564034543 ) ) ;
#9842=DIRECTION ( 'NONE',  ( 0.7071067811865486830, -0.7071067811865464625, -0.000000000000000000 ) ) ;
#9843=CARTESIAN_POINT ( 'NONE',  ( -32.67183060077623935, 2.259292476615694323, 4.000000000000000000 ) ) ;
#9844=DIRECTION ( 'NONE',  ( 0.7071067811865487940, 0.7071067811865463515, 0.000000000000000000 ) ) ;
#9845=CARTESIAN_POINT ( 'NONE',  ( 34.49999999999975131, -5.568876922607759461, 4.000000000000000000 ) ) ;
#9846=ORIENTED_EDGE ( 'NONE', *, *, #35728, .F. ) ;
#9848=CARTESIAN_POINT ( 'NONE',  ( -21.18398860626899349, 28.73617430169802134, 5.000000000000000000 ) ) ;
#9849=AXIS2_PLACEMENT_3D ( 'NONE', #121094, #141432, #87053 ) ;
#9850=CARTESIAN_POINT ( 'NONE',  ( 31.82816939922330945, 6.759292476615649470, 4.000000000000000000 ) ) ;
#9851=PLANE ( 'NONE',  #57726 ) ;
#9853=EDGE_CURVE ( 'NONE', #55021, #47967, #119074, .T. ) ;
#9856=ORIENTED_EDGE ( 'NONE', *, *, #40724, .F. ) ;
#9857=CARTESIAN_POINT ( 'NONE',  ( -9.498163485139505369, -17.24070752338410273, 8.407044977365249139 ) ) ;
#9858=DIRECTION ( 'NONE',  ( -0.000000000000000000, 0.3543493200069153248, 0.9351131265310292928 ) ) ;
#9861=ORIENTED_EDGE ( 'NONE', *, *, #1188, .T. ) ;
#9862=VECTOR ( 'NONE', #84857, 1000.000000000000000 ) ;
#9863=AXIS2_PLACEMENT_3D ( 'NONE', #4469, #57522, #125628 ) ;
#9864=LINE ( 'NONE', #44697, #5135 ) ;
#9866=VECTOR ( 'NONE', #128692, 1000.000000000000227 ) ;
#9867=VECTOR ( 'NONE', #27923, 1000.000000000000000 ) ;
#9870=VECTOR ( 'NONE', #108772, 999.9999999999998863 ) ;
#9872=LINE ( 'NONE', #20020, #47061 ) ;
#9874=ORIENTED_EDGE ( 'NONE', *, *, #79413, .F. ) ;
#9875=VERTEX_POINT ( 'NONE', #96576 ) ;
#9876=FACE_OUTER_BOUND ( 'NONE', #72613, .T. ) ;
#9878=DIRECTION ( 'NONE',  ( 0.6830127018922181881, 0.6830127018922202975, -0.2588190451025214056 ) ) ;
#9880=DIRECTION ( 'NONE',  ( -0.000000000000000000, 0.000000000000000000, 1.000000000000000000 ) ) ;
#9882=VERTEX_POINT ( 'NONE', #74165 ) ;
#9886=ORIENTED_EDGE ( 'NONE', *, *, #138597, .F. ) ;
#9887=VERTEX_POINT ( 'NONE', #64003 ) ;
#9889=AXIS2_PLACEMENT_3D ( 'NONE', #25255, #23843, #3482 ) ;
#9890=DIRECTION ( 'NONE',  ( -0.7071067811865486830, -0.7071067811865464625, -0.000000000000000000 ) ) ;
#9891=LINE ( 'NONE', #30222, #21629 ) ;
#9892=ADVANCED_FACE ( 'NONE', ( #52392 ), #29919, .T. ) ;
#9893=ORIENTED_EDGE ( 'NONE', *, *, #101893, .T. ) ;
#9894=LINE ( 'NONE', #8430, #48281 ) ;
#9895=CARTESIAN_POINT ( 'NONE',  ( -32.99999999999976552, 14.87792677143806230, -11.06722581663447791 ) ) ;
#9897=CARTESIAN_POINT ( 'NONE',  ( -30.18398860626900060, 28.73617430169808173, 5.000000000000000000 ) ) ;
#9898=DIRECTION ( 'NONE',  ( -0.7071067811865486830, -0.7071067811865464625, -0.000000000000000000 ) ) ;
#9900=AXIS2_PLACEMENT_3D ( 'NONE', #99895, #76745, #21628 ) ;
#9902=EDGE_LOOP ( 'NONE', ( #121830, #60802, #62152, #63968 ) ) ;
#9903=LINE ( 'NONE', #29505, #3247 ) ;
#9904=LINE ( 'NONE', #142586, #18755 ) ;
#9905=EDGE_CURVE ( 'NONE', #108536, #33945, #41513, .T. ) ;
#9906=VERTEX_POINT ( 'NONE', #97297 ) ;
#9907=ORIENTED_EDGE ( 'NONE', *, *, #17531, .F. ) ;
#9909=EDGE_CURVE ( 'NONE', #121879, #112076, #31372, .T. ) ;
#9910=VERTEX_POINT ( 'NONE', #39880 ) ;
#9912=VERTEX_POINT ( 'NONE', #84780 ) ;
#9913=VECTOR ( 'NONE', #31915, 1000.000000000000114 ) ;
#9914=EDGE_CURVE ( 'NONE', #71118, #8088, #61632, .T. ) ;
#9915=EDGE_CURVE ( 'NONE', #76248, #30378, #106490, .T. ) ;
#9916=DIRECTION ( 'NONE',  ( 0.7071067811865487940, 0.7071067811865463515, 0.000000000000000000 ) ) ;
#9920=EDGE_CURVE ( 'NONE', #31242, #127932, #41259, .T. ) ;
#9921=AXIS2_PLACEMENT_3D ( 'NONE', #3962, #59843, #104010 ) ;
#9922=ORIENTED_EDGE ( 'NONE', *, *, #51040, .F. ) ;
#9925=EDGE_CURVE ( 'NONE', #3772, #27504, #70103, .T. ) ;
#9926=CARTESIAN_POINT ( 'NONE',  ( 2.994519915287485734, 28.92564299267940342, 4.000000000000000000 ) ) ;
#9927=CARTESIAN_POINT ( 'NONE',  ( 18.18398860626898994, 28.73617430169800002, 5.000000000000000000 ) ) ;
#9928=CARTESIAN_POINT ( 'NONE',  ( 60.18398860626900415, 28.73617430169829490, 5.000000000000000000 ) ) ;
#9929=ADVANCED_FACE ( 'NONE', ( #129695 ), #49333, .F. ) ;
#9930=ORIENTED_EDGE ( 'NONE', *, *, #139893, .F. ) ;
#9931=ORIENTED_EDGE ( 'NONE', *, *, #6302, .F. ) ;
#9932=ORIENTED_EDGE ( 'NONE', *, *, #111355, .F. ) ;
#9933=VERTEX_POINT ( 'NONE', #60941 ) ;
#9936=ORIENTED_EDGE ( 'NONE', *, *, #90310, .F. ) ;
#9937=CARTESIAN_POINT ( 'NONE',  ( -12.18398860626900060, 28.73617430169795739, 5.000000000000000000 ) ) ;
#9938=EDGE_CURVE ( 'NONE', #129447, #16801, #6449, .T. ) ;
#9939=DIRECTION ( 'NONE',  ( -0.6830127018922181881, 0.6830127018922202975, -0.2588190451025214056 ) ) ;
#9940=VERTEX_POINT ( 'NONE', #73906 ) ;
#9941=CARTESIAN_POINT ( 'NONE',  ( 33.48921356237309510, -27.52281430457078670, 5.000000000000000000 ) ) ;
#9942=VECTOR ( 'NONE', #111478, 1000.000000000000000 ) ;
#9943=EDGE_LOOP ( 'NONE', ( #69719, #67387, #12799, #123595 ) ) ;
#9944=EDGE_CURVE ( 'NONE', #79175, #14571, #139899, .T. ) ;
#9946=DIRECTION ( 'NONE',  ( 0.7071067811865486830, -0.7071067811865464625, -0.000000000000000000 ) ) ;
#9951=ADVANCED_FACE ( 'NONE', ( #83362 ), #38430, .F. ) ;
#9952=VERTEX_POINT ( 'NONE', #84103 ) ;
#9957=PLANE ( 'NONE',  #59896 ) ;
#9958=VECTOR ( 'NONE', #116929, 1000.000000000000227 ) ;
#9959=VECTOR ( 'NONE', #24888, 999.9999999999998863 ) ;
#9960=EDGE_CURVE ( 'NONE', #70528, #58012, #107234, .T. ) ;
#9961=CARTESIAN_POINT ( 'NONE',  ( -5.207106781186506161, -17.24070752338410628, 5.000000000000000000 ) ) ;
#9963=DIRECTION ( 'NONE',  ( 0.7071067811865487940, -0.7071067811865463515, 0.000000000000000000 ) ) ;
#9964=DIRECTION ( 'NONE',  ( 0.000000000000000000, 0.000000000000000000, -1.000000000000000000 ) ) ;
#9965=EDGE_CURVE ( 'NONE', #73925, #97534, #115954, .T. ) ;
#9967=LINE ( 'NONE', #7815, #120384 ) ;
#9968=VECTOR ( 'NONE', #118329, 1000.000000000000000 ) ;
#9969=VECTOR ( 'NONE', #16830, 1000.000000000000000 ) ;
#9971=ORIENTED_EDGE ( 'NONE', *, *, #84467, .T. ) ;
#9972=CARTESIAN_POINT ( 'NONE',  ( 18.70710678118641468, 11.25929247661559529, 5.000000000000000000 ) ) ;
#9973=ORIENTED_EDGE ( 'NONE', *, *, #131895, .T. ) ;
#9975=FACE_OUTER_BOUND ( 'NONE', #124717, .T. ) ;
#9976=DIRECTION ( 'NONE',  ( 0.7071067811865487940, 0.7071067811865463515, -0.000000000000000000 ) ) ;
#9977=ORIENTED_EDGE ( 'NONE', *, *, #110062, .T. ) ;
#9979=ORIENTED_EDGE ( 'NONE', *, *, #5329, .T. ) ;
#9981=VERTEX_POINT ( 'NONE', #52148 ) ;
#9982=FACE_OUTER_BOUND ( 'NONE', #66996, .T. ) ;
#9984=ORIENTED_EDGE ( 'NONE', *, *, #24077, .T. ) ;
#9990=VECTOR ( 'NONE', #134272, 999.9999999999998863 ) ;
#9991=LINE ( 'NONE', #75277, #87633 ) ;
#9992=ADVANCED_FACE ( 'NONE', ( #39145 ), #127575, .F. ) ;
#9993=LINE ( 'NONE', #86860, #74635 ) ;
#9994=CARTESIAN_POINT ( 'NONE',  ( -31.82816939922330235, -2.240707523384260824, 4.000000000000000000 ) ) ;
#9995=CARTESIAN_POINT ( 'NONE',  ( -5.331532588401397099, -18.74070752338408496, 20.73178291233839943 ) ) ;
#9999=DIRECTION ( 'NONE',  ( 0.6830127018922181881, 0.6830127018922202975, -0.2588190451025214056 ) ) ;
#10000=ORIENTED_EDGE ( 'NONE', *, *, #78306, .F. ) ;
#10001=VECTOR ( 'NONE', #128689, 1000.000000000000114 ) ;
#10002=VERTEX_POINT ( 'NONE', #28978 ) ;
#10003=CARTESIAN_POINT ( 'NONE',  ( 2.292986735706931345, -21.74070752338405654, 4.999753212805221558 ) ) ;
#10006=EDGE_CURVE ( 'NONE', #112008, #80926, #62338, .T. ) ;
#10007=VECTOR ( 'NONE', #73445, 1000.000000000000000 ) ;
#10008=LINE ( 'NONE', #30336, #96541 ) ;
#10011=VERTEX_POINT ( 'NONE', #29663 ) ;
#10012=CARTESIAN_POINT ( 'NONE',  ( 0.1839886062690032631, 28.73617430169787568, 5.000000000000000000 ) ) ;
#10014=VECTOR ( 'NONE', #28700, 999.9999999999998863 ) ;
#10015=CARTESIAN_POINT ( 'NONE',  ( 63.18398860626900415, 28.73617430169831621, 5.000000000000000000 ) ) ;
#10020=FACE_OUTER_BOUND ( 'NONE', #24090, .T. ) ;
#10022=DIRECTION ( 'NONE',  ( 0.7071067811865486830, -0.7071067811865464625, -0.000000000000000000 ) ) ;
#10023=CARTESIAN_POINT ( 'NONE',  ( 11.29289321881337571, 17.25929247661554200, 5.000000000000000000 ) ) ;
#10024=FACE_OUTER_BOUND ( 'NONE', #117440, .T. ) ;
#10025=CIRCLE ( 'NONE', #95701, 5.968999999999998529 ) ;
#10026=ORIENTED_EDGE ( 'NONE', *, *, #5178, .T. ) ;
#10027=VERTEX_POINT ( 'NONE', #37256 ) ;
#10030=VECTOR ( 'NONE', #98921, 1000.000000000000000 ) ;
#10031=ORIENTED_EDGE ( 'NONE', *, *, #39591, .T. ) ;
#10034=CARTESIAN_POINT ( 'NONE',  ( 16.49999999999988631, 19.39370406404968605, 1.459788787078164063 ) ) ;
#10035=VERTEX_POINT ( 'NONE', #92321 ) ;
#10036=CARTESIAN_POINT ( 'NONE',  ( -21.88837638105228933, 9.759292476615614831, 17.35367589129217691 ) ) ;
#10037=DIRECTION ( 'NONE',  ( 0.7071067811865486830, -0.7071067811865464625, -0.000000000000000000 ) ) ;
#10038=ADVANCED_FACE ( 'NONE', ( #4551 ), #114781, .F. ) ;
#10041=VERTEX_POINT ( 'NONE', #139460 ) ;
#10042=DIRECTION ( 'NONE',  ( 0.7071067811865486830, -0.7071067811865464625, -0.000000000000000000 ) ) ;
#10043=DIRECTION ( 'NONE',  ( 0.7071067811865487940, 0.7071067811865463515, -0.000000000000000000 ) ) ;
#10045=ORIENTED_EDGE ( 'NONE', *, *, #6613, .T. ) ;
#10046=VERTEX_POINT ( 'NONE', #82219 ) ;
#10047=CARTESIAN_POINT ( 'NONE',  ( -20.99451991528748707, 28.92564299267952777, 4.000000000000000000 ) ) ;
#10048=EDGE_CURVE ( 'NONE', #1418, #54913, #28534, .T. ) ;
#10049=CARTESIAN_POINT ( 'NONE',  ( 26.66989781452719299, 17.25929247661554555, 19.83885114516065329 ) ) ;
#10050=VECTOR ( 'NONE', #136619, 1000.000000000000000 ) ;
#10051=CARTESIAN_POINT ( 'NONE',  ( 9.299744871391588674, -27.71228299555212971, 4.000000000000000000 ) ) ;
#10053=FACE_OUTER_BOUND ( 'NONE', #40201, .T. ) ;
#10055=ORIENTED_EDGE ( 'NONE', *, *, #43353, .F. ) ;
#10056=VERTEX_POINT ( 'NONE', #103208 ) ;
#10057=DIRECTION ( 'NONE',  ( -0.000000000000000000, 0.000000000000000000, 1.000000000000000000 ) ) ;
#10058=ORIENTED_EDGE ( 'NONE', *, *, #3567, .F. ) ;
#10059=ORIENTED_EDGE ( 'NONE', *, *, #74856, .F. ) ;
#10060=AXIS2_PLACEMENT_3D ( 'NONE', #807, #112454, #121871 ) ;
#10061=CARTESIAN_POINT ( 'NONE',  ( 15.13014816246815109, 7.677378749015542070, 4.326165144404741092 ) ) ;
#10063=ORIENTED_EDGE ( 'NONE', *, *, #32221, .F. ) ;
#10066=DIRECTION ( 'NONE',  ( 0.3543493200069162685, -0.000000000000000000, -0.9351131265310288487 ) ) ;
#10067=LINE ( 'NONE', #99949, #143281 ) ;
#10068=LINE ( 'NONE', #53602, #134631 ) ;
#10069=VERTEX_POINT ( 'NONE', #138722 ) ;
#10073=VERTEX_POINT ( 'NONE', #82915 ) ;
#10074=DIRECTION ( 'NONE',  ( 0.7071067811865487940, 0.7071067811865463515, -0.000000000000000000 ) ) ;
#10075=EDGE_CURVE ( 'NONE', #130332, #19651, #27079, .T. ) ;
#10076=ORIENTED_EDGE ( 'NONE', *, *, #107350, .F. ) ;
#10077=CARTESIAN_POINT ( 'NONE',  ( -9.183988606268997046, 28.73617430169793607, 5.000000000000000000 ) ) ;
#10078=ORIENTED_EDGE ( 'NONE', *, *, #41116, .F. ) ;
#10079=ORIENTED_EDGE ( 'NONE', *, *, #75503, .T. ) ;
#10081=ORIENTED_EDGE ( 'NONE', *, *, #53, .T. ) ;
#10082=ADVANCED_FACE ( 'NONE', ( #17613 ), #115479, .F. ) ;
#10083=ADVANCED_FACE ( 'NONE', ( #81504 ), #5310, .T. ) ;
#10084=CARTESIAN_POINT ( 'NONE',  ( -33.70710678118631165, -0.7407075233842788098, 5.000000000000000000 ) ) ;
#10085=PLANE ( 'NONE',  #38286 ) ;
#10087=DIRECTION ( 'NONE',  ( 0.6830127018922180770, -0.6830127018922204085, -0.2588190451025213501 ) ) ;
#10088=CARTESIAN_POINT ( 'NONE',  ( 25.49999999999982947, -7.420205493532873398, -2.617629953481194871 ) ) ;
#10091=FACE_OUTER_BOUND ( 'NONE', #107438, .T. ) ;
#10092=EDGE_CURVE ( 'NONE', #71076, #135550, #93776, .T. ) ;
#10093=PLANE ( 'NONE',  #108425 ) ;
#10094=EDGE_CURVE ( 'NONE', #76593, #51414, #70639, .T. ) ;
#10095=AXIS2_PLACEMENT_3D ( 'NONE', #34212, #57405, #111018 ) ;
#10096=CARTESIAN_POINT ( 'NONE',  ( 0.3281693992235254487, -21.74070752338406365, 4.000000000000000000 ) ) ;
#10097=PLANE ( 'NONE',  #15774 ) ;
#10098=EDGE_CURVE ( 'NONE', #91612, #106603, #138001, .T. ) ;
#10099=DIRECTION ( 'NONE',  ( 0.3543493200069162685, -0.000000000000000000, -0.9351131265310288487 ) ) ;
#10100=AXIS2_PLACEMENT_3D ( 'NONE', #21185, #8825, #131388 ) ;
#10102=EDGE_LOOP ( 'NONE', ( #30870, #91775, #48933, #52954 ) ) ;
#10104=ORIENTED_EDGE ( 'NONE', *, *, #84010, .F. ) ;
#10105=DIRECTION ( 'NONE',  ( -0.000000000000000000, -0.3543493200069152693, 0.9351131265310292928 ) ) ;
#10106=ORIENTED_EDGE ( 'NONE', *, *, #66644, .T. ) ;
#10108=ORIENTED_EDGE ( 'NONE', *, *, #101234, .T. ) ;
#10109=DIRECTION ( 'NONE',  ( -0.3543493200069163240, 0.000000000000000000, -0.9351131265310288487 ) ) ;
#10110=PLANE ( 'NONE',  #114937 ) ;
#10112=EDGE_CURVE ( 'NONE', #79734, #75031, #73462, .T. ) ;
#10113=CARTESIAN_POINT ( 'NONE',  ( 10.49999999999992184, 1.087461875839246250, 4.000000000000000000 ) ) ;
#10114=ORIENTED_EDGE ( 'NONE', *, *, #105560, .T. ) ;
#10115=DIRECTION ( 'NONE',  ( 0.6830127018922180770, -0.6830127018922204085, -0.2588190451025213501 ) ) ;
#10116=ORIENTED_EDGE ( 'NONE', *, *, #54417, .T. ) ;
#10117=ADVANCED_FACE ( 'NONE', ( #93061 ), #16930, .F. ) ;
#10118=CARTESIAN_POINT ( 'NONE',  ( -57.18398860626899705, 28.73617430169827358, 5.000000000000000000 ) ) ;
#10119=AXIS2_PLACEMENT_3D ( 'NONE', #73930, #85493, #129723 ) ;
#10120=DIRECTION ( 'NONE',  ( 0.7071067811865487940, 0.7071067811865463515, 0.000000000000000000 ) ) ;
#10123=EDGE_LOOP ( 'NONE', ( #81479, #59874, #123826, #128827 ) ) ;
#10126=CARTESIAN_POINT ( 'NONE',  ( -48.48921356237309510, -27.52281430457089328, 5.000000000000000000 ) ) ;
#10130=VERTEX_POINT ( 'NONE', #6006 ) ;
#10131=ORIENTED_EDGE ( 'NONE', *, *, #63865, .T. ) ;
#10132=CARTESIAN_POINT ( 'NONE',  ( 31.49999999999977973, 13.08746187583911436, 4.000000000000000000 ) ) ;
#10133=VECTOR ( 'NONE', #19968, 1000.000000000000000 ) ;
#10134=CARTESIAN_POINT ( 'NONE',  ( -20.56319896779158185, -12.74070752338415069, 9.898150129686422716 ) ) ;
#10135=DIRECTION ( 'NONE',  ( -0.6830127018922180770, -0.6830127018922204085, -0.2588190451025213501 ) ) ;
#10136=FACE_OUTER_BOUND ( 'NONE', #127618, .T. ) ;
#10137=ORIENTED_EDGE ( 'NONE', *, *, #93045, .F. ) ;
#10139=CARTESIAN_POINT ( 'NONE',  ( 56.99451991528749062, 28.92564299267978001, 4.000000000000000000 ) ) ;
#10140=ADVANCED_FACE ( 'NONE', ( #50282 ), #94472, .F. ) ;
#10141=ORIENTED_EDGE ( 'NONE', *, *, #137673, .T. ) ;
#10144=CARTESIAN_POINT ( 'NONE',  ( 18.18398860626898994, 28.73617430169800002, 5.000000000000000000 ) ) ;
#10145=ORIENTED_EDGE ( 'NONE', *, *, #49440, .F. ) ;
#10146=CARTESIAN_POINT ( 'NONE',  ( -36.18398860626899705, 28.73617430169812437, 5.000000000000000000 ) ) ;
#10147=ORIENTED_EDGE ( 'NONE', *, *, #88004, .F. ) ;
#10148=ORIENTED_EDGE ( 'NONE', *, *, #127231, .T. ) ;
#10149=PLANE ( 'NONE',  #123488 ) ;
#10151=ORIENTED_EDGE ( 'NONE', *, *, #8457, .F. ) ;
#10152=FACE_OUTER_BOUND ( 'NONE', #48320, .T. ) ;
#10153=EDGE_CURVE ( 'NONE', #63922, #42670, #30678, .T. ) ;
#10154=CARTESIAN_POINT ( 'NONE',  ( 1.499999999999984013, 14.14708470758591474, -0.5283514160166593587 ) ) ;
#10155=CARTESIAN_POINT ( 'NONE',  ( -33.18398860626899705, 28.73617430169810305, 5.000000000000000000 ) ) ;
#10156=VECTOR ( 'NONE', #102501, 1000.000000000000000 ) ;
#10157=DIRECTION ( 'NONE',  ( 0.6830127018922180770, -0.6830127018922204085, -0.2588190451025213501 ) ) ;
#10158=DIRECTION ( 'NONE',  ( 0.7071067811865487940, 0.7071067811865463515, -0.000000000000000000 ) ) ;
#10159=EDGE_CURVE ( 'NONE', #118849, #100584, #131405, .T. ) ;
#10160=CARTESIAN_POINT ( 'NONE',  ( -26.99999999999981526, 10.93112307739207267, 4.000000000000000000 ) ) ;
#10161=CARTESIAN_POINT ( 'NONE',  ( 21.18398860626899349, 28.73617430169802134, 5.000000000000000000 ) ) ;
#10162=CARTESIAN_POINT ( 'NONE',  ( 18.12391743882421480, 22.22500000000000142, -15.10221789024010874 ) ) ;
#10163=CARTESIAN_POINT ( 'NONE',  ( -35.39513766812457618, 21.75929247661549226, 21.32995629748194588 ) ) ;
#10164=CARTESIAN_POINT ( 'NONE',  ( 32.99999999999977973, -8.731860332648809120, -2.120594902707463536 ) ) ;
#10165=CARTESIAN_POINT ( 'NONE',  ( 21.51665438641029482, 22.22500000000000142, 4.500000000000000888 ) ) ;
#10166=CARTESIAN_POINT ( 'NONE',  ( -33.81246187583924012, -22.22500000000000142, 4.000000000000000000 ) ) ;
#10167=ORIENTED_EDGE ( 'NONE', *, *, #42849, .T. ) ;
#10168=VECTOR ( 'NONE', #54170, 999.9999999999998863 ) ;
#10169=ORIENTED_EDGE ( 'NONE', *, *, #1232, .F. ) ;
#10171=ORIENTED_EDGE ( 'NONE', *, *, #49256, .T. ) ;
#10172=EDGE_LOOP ( 'NONE', ( #127159, #89750, #35819, #50662 ) ) ;
#10173=EDGE_CURVE ( 'NONE', #32103, #116900, #41517, .T. ) ;
#10175=CARTESIAN_POINT ( 'NONE',  ( 42.48921356237308800, -27.52281430457085065, 5.000000000000000000 ) ) ;
#10176=CARTESIAN_POINT ( 'NONE',  ( 32.99999999999977263, 19.93112307739198030, 4.000000000000000000 ) ) ;
#10178=CARTESIAN_POINT ( 'NONE',  ( 6.328169399223481761, -3.740707523384245281, 4.000000000000000000 ) ) ;
#10180=PLANE ( 'NONE',  #124 ) ;
#10181=CARTESIAN_POINT ( 'NONE',  ( -72.18398860626899705, 28.73617430169837661, 5.000000000000000000 ) ) ;
#10182=EDGE_CURVE ( 'NONE', #38066, #82163, #21203, .T. ) ;
#10185=PLANE ( 'NONE',  #105186 ) ;
#10186=VECTOR ( 'NONE', #87313, 1000.000000000000000 ) ;
#10191=DIRECTION ( 'NONE',  ( 0.7071067811865487940, 0.7071067811865463515, 0.000000000000000000 ) ) ;
#10192=EDGE_CURVE ( 'NONE', #133341, #75052, #95907, .T. ) ;
#10193=EDGE_LOOP ( 'NONE', ( #97808, #134758, #31535, #117418 ) ) ;
#10194=ORIENTED_EDGE ( 'NONE', *, *, #99181, .F. ) ;
#10196=ORIENTED_EDGE ( 'NONE', *, *, #1616, .T. ) ;
#10198=CARTESIAN_POINT ( 'NONE',  ( -36.48921356237310221, -27.52281430457080802, 5.000000000000000000 ) ) ;
#10199=DIRECTION ( 'NONE',  ( -0.7071067811865487940, 0.7071067811865463515, -0.000000000000000000 ) ) ;
#10200=CARTESIAN_POINT ( 'NONE',  ( 17.29320749275915148, 20.25929247661551358, 20.83292124670811063 ) ) ;
#10205=VECTOR ( 'NONE', #95537, 1000.000000000000000 ) ;
#10206=EDGE_LOOP ( 'NONE', ( #16319, #14721, #22641, #97990 ) ) ;
#10211=( BOUNDED_CURVE ( )  B_SPLINE_CURVE ( 3, ( #132166, #30715, #54601, #77777 ),
 .UNSPECIFIED., .F., .T. ) 
 B_SPLINE_CURVE_WITH_KNOTS ( ( 4, 4 ),
 ( 5.920967161967926273, 7.341195215986634715 ),
 .UNSPECIFIED. ) 
 CURVE ( )  GEOMETRIC_REPRESENTATION_ITEM ( )  RATIONAL_B_SPLINE_CURVE ( ( 1.000000000000000000, 0.8388583629366618277, 0.8388583629366618277, 1.000000000000000000 ) ) 
 REPRESENTATION_ITEM ( '' )  );
#10213=ORIENTED_EDGE ( 'NONE', *, *, #109440, .T. ) ;
#10215=VECTOR ( 'NONE', #132834, 1000.000000000000000 ) ;
#10217=FACE_OUTER_BOUND ( 'NONE', #130782, .T. ) ;
#10218=EDGE_CURVE ( 'NONE', #1803, #74547, #53864, .T. ) ;
#10219=DIRECTION ( 'NONE',  ( 0.7071067811865487940, 0.7071067811865463515, -0.000000000000000000 ) ) ;
#10220=DIRECTION ( 'NONE',  ( -0.6830127018922181881, 0.6830127018922202975, -0.2588190451025214056 ) ) ;
#10221=AXIS2_PLACEMENT_3D ( 'NONE', #115788, #18630, #5617 ) ;
#10224=VERTEX_POINT ( 'NONE', #120475 ) ;
#10225=DIRECTION ( 'NONE',  ( 0.3543493200069162685, -0.000000000000000000, -0.9351131265310288487 ) ) ;
#10226=VERTEX_POINT ( 'NONE', #10312 ) ;
#10228=ORIENTED_EDGE ( 'NONE', *, *, #135474, .T. ) ;
#10230=DIRECTION ( 'NONE',  ( -0.6830127018922180770, -0.6830127018922204085, -0.2588190451025213501 ) ) ;
#10231=CARTESIAN_POINT ( 'NONE',  ( 17.99451991528748351, 28.92564299267950645, 4.000000000000000000 ) ) ;
#10232=VERTEX_POINT ( 'NONE', #32087 ) ;
#10234=CARTESIAN_POINT ( 'NONE',  ( 24.85005128541009611, -8.240707523384189770, 17.25253755692244795 ) ) ;
#10236=DIRECTION ( 'NONE',  ( 0.7071067811865486830, -0.7071067811865464625, -0.000000000000000000 ) ) ;
#10237=FACE_OUTER_BOUND ( 'NONE', #3209, .T. ) ;
#10238=FACE_BOUND ( 'NONE', #31698, .T. ) ;
#10240=CARTESIAN_POINT ( 'NONE',  ( 13.17183060077638679, -2.240707523384255939, 4.000000000000000000 ) ) ;
#10243=ORIENTED_EDGE ( 'NONE', *, *, #19404, .T. ) ;
#10244=PLANE ( 'NONE',  #31849 ) ;
#10247=DIRECTION ( 'NONE',  ( -0.7071067811865487940, 0.7071067811865463515, -0.000000000000000000 ) ) ;
#10248=ORIENTED_EDGE ( 'NONE', *, *, #46903, .T. ) ;
#10249=ADVANCED_FACE ( 'NONE', ( #142294 ), #98749, .F. ) ;
#10251=ORIENTED_EDGE ( 'NONE', *, *, #78707, .T. ) ;
#10252=DIRECTION ( 'NONE',  ( -0.7071067811865487940, 0.7071067811865463515, 0.000000000000000000 ) ) ;
#10253=ADVANCED_FACE ( 'NONE', ( #129975 ), #97301, .F. ) ;
#10255=DIRECTION ( 'NONE',  ( -0.000000000000000000, 0.3543493200069153248, 0.9351131265310292928 ) ) ;
#10256=ORIENTED_EDGE ( 'NONE', *, *, #95497, .T. ) ;
#10257=EDGE_CURVE ( 'NONE', #133408, #13443, #119773, .T. ) ;
#10258=FACE_OUTER_BOUND ( 'NONE', #122651, .T. ) ;
#10260=VECTOR ( 'NONE', #89953, 1000.000000000000000 ) ;
#10261=CARTESIAN_POINT ( 'NONE',  ( -39.48921356237310221, -27.52281430457082934, 5.000000000000000000 ) ) ;
#10262=CARTESIAN_POINT ( 'NONE',  ( -45.18398860626900415, 28.73617430169818832, 5.000000000000000000 ) ) ;
#10264=FACE_OUTER_BOUND ( 'NONE', #128408, .T. ) ;
#10265=LINE ( 'NONE', #107443, #16266 ) ;
#10266=VERTEX_POINT ( 'NONE', #119080 ) ;
#10267=ORIENTED_EDGE ( 'NONE', *, *, #15900, .T. ) ;
#10268=ORIENTED_EDGE ( 'NONE', *, *, #14239, .F. ) ;
#10269=CARTESIAN_POINT ( 'NONE',  ( 3.469446951953614189E-15, -7.447814304570758104, 5.000000000000000000 ) ) ;
#10270=CARTESIAN_POINT ( 'NONE',  ( -9.792893218813388145, 12.75929247661558996, 5.000000000000000000 ) ) ;
#10271=ORIENTED_EDGE ( 'NONE', *, *, #54787, .T. ) ;
#10272=ORIENTED_EDGE ( 'NONE', *, *, #71794, .F. ) ;
#10273=LINE ( 'NONE', #63289, #9575 ) ;
#10274=CARTESIAN_POINT ( 'NONE',  ( 14.67183060077637613, 11.25929247661561128, 4.000000000000000000 ) ) ;
#10275=ADVANCED_FACE ( 'NONE', ( #31377 ), #109638, .F. ) ;
#10276=EDGE_CURVE ( 'NONE', #16863, #7658, #19770, .T. ) ;
#10277=LINE ( 'NONE', #54536, #111061 ) ;
#10278=ORIENTED_EDGE ( 'NONE', *, *, #97038, .F. ) ;
#10279=LINE ( 'NONE', #132826, #134255 ) ;
#10281=EDGE_CURVE ( 'NONE', #61260, #107902, #29925, .T. ) ;
#10282=CARTESIAN_POINT ( 'NONE',  ( -75.48921356237309510, -27.52281430457107803, 5.000000000000000000 ) ) ;
#10283=VECTOR ( 'NONE', #25345, 1000.000000000000000 ) ;
#10286=ORIENTED_EDGE ( 'NONE', *, *, #34526, .F. ) ;
#10288=AXIS2_PLACEMENT_3D ( 'NONE', #14089, #82248, #135889 ) ;
#10289=CARTESIAN_POINT ( 'NONE',  ( 6.183988606268994381, 28.73617430169791476, 5.000000000000000000 ) ) ;
#10290=LINE ( 'NONE', #40118, #135264 ) ;
#10292=CARTESIAN_POINT ( 'NONE',  ( -19.05000000000000071, 3.174999999999997158, 5.000000000000000000 ) ) ;
#10293=EDGE_LOOP ( 'NONE', ( #47735, #44106, #135895 ) ) ;
#10294=CARTESIAN_POINT ( 'NONE',  ( -21.32816939922336985, -18.74070752338409207, 4.000000000000000000 ) ) ;
#10296=DIRECTION ( 'NONE',  ( -0.6830127018922181881, 0.6830127018922202975, -0.2588190451025214056 ) ) ;
#10297=CARTESIAN_POINT ( 'NONE',  ( -24.70612307739178348, 22.22500000000000142, 4.000000000000000000 ) ) ;
#10298=DIRECTION ( 'NONE',  ( 1.000000000000000000, 0.000000000000000000, 0.000000000000000000 ) ) ;
#10300=VECTOR ( 'NONE', #103376, 1000.000000000000000 ) ;
#10301=LINE ( 'NONE', #63314, #125163 ) ;
#10302=PLANE ( 'NONE',  #83770 ) ;
#10303=ADVANCED_FACE ( 'NONE', ( #52396 ), #96581, .F. ) ;
#10304=EDGE_LOOP ( 'NONE', ( #45505, #86295, #117562, #20927 ) ) ;
#10305=DIRECTION ( 'NONE',  ( 0.7071067811865487940, 0.7071067811865463515, -0.000000000000000000 ) ) ;
#10308=DIRECTION ( 'NONE',  ( -0.7071067811865486830, 0.7071067811865464625, 0.000000000000000000 ) ) ;
#10309=CARTESIAN_POINT ( 'NONE',  ( 21.56169048593611137, 22.22500000000000142, -16.40491860849569861 ) ) ;
#10310=ORIENTED_EDGE ( 'NONE', *, *, #25926, .F. ) ;
#10311=EDGE_LOOP ( 'NONE', ( #78106, #133887, #11946, #39924 ) ) ;
#10312=CARTESIAN_POINT ( 'NONE',  ( -19.49999999999986144, 9.431123077392085108, 4.000000000000000000 ) ) ;
#10313=CARTESIAN_POINT ( 'NONE',  ( 37.40832548098978094, -0.7407075233842770334, 14.76736230305389341 ) ) ;
#10314=VERTEX_POINT ( 'NONE', #58168 ) ;
#10315=VECTOR ( 'NONE', #7022, 1000.000000000000000 ) ;
#10317=DIRECTION ( 'NONE',  ( 0.7071067811865486830, -0.7071067811865464625, -0.000000000000000000 ) ) ;
#10318=AXIS2_PLACEMENT_3D ( 'NONE', #81860, #91301, #102873 ) ;
#10320=LINE ( 'NONE', #142990, #56169 ) ;
#10321=ORIENTED_EDGE ( 'NONE', *, *, #65043, .F. ) ;
#10324=DIRECTION ( 'NONE',  ( -0.6830127018922181881, 0.6830127018922202975, -0.2588190451025214056 ) ) ;
#10325=DIRECTION ( 'NONE',  ( 0.7071067811865487940, 0.7071067811865463515, -0.000000000000000000 ) ) ;
#10328=CARTESIAN_POINT ( 'NONE',  ( -31.49999999999977973, 12.43112307739205669, 4.000000000000000000 ) ) ;
#10331=VERTEX_POINT ( 'NONE', #46587 ) ;
#10332=CARTESIAN_POINT ( 'NONE',  ( -8.292893218813393474, -12.74070752338415247, 5.000000000000000000 ) ) ;
#10334=EDGE_CURVE ( 'NONE', #113756, #98208, #114503, .T. ) ;
#10335=ORIENTED_EDGE ( 'NONE', *, *, #24904, .F. ) ;
#10336=CARTESIAN_POINT ( 'NONE',  ( 0.000000000000000000, 0.000000000000000000, 5.000000000000000000 ) ) ;
#10337=DIRECTION ( 'NONE',  ( 0.7071067811865486830, -0.7071067811865464625, -0.000000000000000000 ) ) ;
#10338=ORIENTED_EDGE ( 'NONE', *, *, #14548, .F. ) ;
#10341=DIRECTION ( 'NONE',  ( 0.7071067811865486830, -0.7071067811865464625, -0.000000000000000000 ) ) ;
#10342=LINE ( 'NONE', #132162, #55725 ) ;
#10345=ORIENTED_EDGE ( 'NONE', *, *, #3389, .F. ) ;
#10346=DIRECTION ( 'NONE',  ( -0.6830127018922181881, 0.6830127018922202975, -0.2588190451025214056 ) ) ;
#10348=CARTESIAN_POINT ( 'NONE',  ( -72.18398860626899705, 28.73617430169837661, 5.000000000000000000 ) ) ;
#10349=DIRECTION ( 'NONE',  ( 0.7071067811865487940, 0.7071067811865463515, 0.000000000000000000 ) ) ;
#10350=DIRECTION ( 'NONE',  ( 0.6830127018922181881, 0.6830127018922202975, -0.2588190451025214056 ) ) ;
#10351=PLANE ( 'NONE',  #2805 ) ;
#10355=DIRECTION ( 'NONE',  ( 0.6830127018922180770, -0.6830127018922204085, -0.2588190451025213501 ) ) ;
#10356=ORIENTED_EDGE ( 'NONE', *, *, #35545, .F. ) ;
#10357=EDGE_LOOP ( 'NONE', ( #86504, #143092, #33034, #35321 ) ) ;
#10359=PLANE ( 'NONE',  #18387 ) ;
#10360=CARTESIAN_POINT ( 'NONE',  ( -21.71230993966013045, -21.73547319004781642, 4.999917730833664642 ) ) ;
#10361=EDGE_LOOP ( 'NONE', ( #120112, #35094, #135684, #973 ) ) ;
#10362=CARTESIAN_POINT ( 'NONE',  ( -57.48921356237308800, -27.52281430457095368, 5.000000000000000000 ) ) ;
#10363=AXIS2_PLACEMENT_3D ( 'NONE', #136323, #80547, #1501 ) ;
#10364=PLANE ( 'NONE',  #134922 ) ;
#10366=EDGE_CURVE ( 'NONE', #100225, #25077, #79201, .T. ) ;
#10367=EDGE_LOOP ( 'NONE', ( #43209, #24044, #88520, #29531 ) ) ;
#10370=EDGE_LOOP ( 'NONE', ( #49945, #2289, #140449, #43550 ) ) ;
#10371=PLANE ( 'NONE',  #49274 ) ;
#10372=DIRECTION ( 'NONE',  ( -0.000000000000000000, 0.3543493200069153248, 0.9351131265310292928 ) ) ;
#10373=CARTESIAN_POINT ( 'NONE',  ( 38.99451991528749062, 28.92564299267965211, 4.000000000000000000 ) ) ;
#10374=FACE_OUTER_BOUND ( 'NONE', #42228, .T. ) ;
#10377=FACE_OUTER_BOUND ( 'NONE', #140458, .T. ) ;
#10378=DIRECTION ( 'NONE',  ( 0.3543493200069162685, -0.000000000000000000, -0.9351131265310288487 ) ) ;
#10380=ORIENTED_EDGE ( 'NONE', *, *, #55966, .T. ) ;
#10382=EDGE_CURVE ( 'NONE', #77649, #65242, #90017, .T. ) ;
#10383=CARTESIAN_POINT ( 'NONE',  ( -23.99999999999983302, -21.03360074219752462, 5.000000000000000000 ) ) ;
#10386=CARTESIAN_POINT ( 'NONE',  ( -11.27718569542934191, -21.72500000000000853, 5.000000000000000000 ) ) ;
#10387=AXIS2_PLACEMENT_3D ( 'NONE', #118030, #52788, #74589 ) ;
#10388=EDGE_LOOP ( 'NONE', ( #118476, #139274, #136707, #31168 ) ) ;
#10389=LINE ( 'NONE', #936, #54614 ) ;
#10391=AXIS2_PLACEMENT_3D ( 'NONE', #90434, #134683, #100612 ) ;
#10392=CARTESIAN_POINT ( 'NONE',  ( -27.48921356237309155, -27.52281430457074762, 5.000000000000000000 ) ) ;
#10393=DIRECTION ( 'NONE',  ( 0.7071067811865486830, -0.7071067811865464625, -0.000000000000000000 ) ) ;
#10394=DIRECTION ( 'NONE',  ( -0.000000000000000000, 0.000000000000000000, 1.000000000000000000 ) ) ;
#10395=VERTEX_POINT ( 'NONE', #12457 ) ;
#10397=LINE ( 'NONE', #42359, #53835 ) ;
#10398=EDGE_LOOP ( 'NONE', ( #50520, #116823, #110041, #107520 ) ) ;
#10399=EDGE_CURVE ( 'NONE', #51683, #25180, #56011, .T. ) ;
#10400=VERTEX_POINT ( 'NONE', #100901 ) ;
#10401=VECTOR ( 'NONE', #75274, 999.9999999999998863 ) ;
#10402=FACE_OUTER_BOUND ( 'NONE', #1182, .T. ) ;
#10403=VERTEX_POINT ( 'NONE', #132856 ) ;
#10404=CARTESIAN_POINT ( 'NONE',  ( -13.49999999999991118, -5.568876922607754132, 4.000000000000000000 ) ) ;
#10405=DIRECTION ( 'NONE',  ( -0.000000000000000000, -0.3543493200069152693, 0.9351131265310292928 ) ) ;
#10406=DIRECTION ( 'NONE',  ( -0.3543493200069162685, -0.000000000000000000, -0.9351131265310288487 ) ) ;
#10407=FACE_BOUND ( 'NONE', #76784, .T. ) ;
#10408=CARTESIAN_POINT ( 'NONE',  ( 0.000000000000000000, 0.000000000000000000, 5.000000000000000000 ) ) ;
#10410=CARTESIAN_POINT ( 'NONE',  ( -28.49999999999980460, 8.319652575858361487, -8.582050562765893176 ) ) ;
#10411=DIRECTION ( 'NONE',  ( 0.7071067811865486830, -0.7071067811865464625, -0.000000000000000000 ) ) ;
#10412=ORIENTED_EDGE ( 'NONE', *, *, #94496, .F. ) ;
#10413=CARTESIAN_POINT ( 'NONE',  ( 23.20710678118638626, -8.240707523384200428, 5.000000000000000000 ) ) ;
#10414=AXIS2_PLACEMENT_3D ( 'NONE', #79433, #33064, #109863 ) ;
#10416=VECTOR ( 'NONE', #56168, 999.9999999999998863 ) ;
#10418=EDGE_CURVE ( 'NONE', #101520, #136399, #80603, .T. ) ;
#10419=ORIENTED_EDGE ( 'NONE', *, *, #128655, .F. ) ;
#10422=CARTESIAN_POINT ( 'NONE',  ( -10.49999999999991829, -7.912538124160678699, 4.000000000000000000 ) ) ;
#10423=VECTOR ( 'NONE', #113112, 1000.000000000000000 ) ;
#10424=FACE_OUTER_BOUND ( 'NONE', #65480, .T. ) ;
#10425=EDGE_CURVE ( 'NONE', #6529, #7602, #33544, .T. ) ;
#10426=VERTEX_POINT ( 'NONE', #69017 ) ;
#10428=ADVANCED_FACE ( 'NONE', ( #22596 ), #121920, .F. ) ;
#10430=DIRECTION ( 'NONE',  ( -0.000000000000000000, 0.3543493200069152138, -0.9351131265310292928 ) ) ;
#10431=CARTESIAN_POINT ( 'NONE',  ( 24.15612307739224818, -22.22500000000000142, 4.000000000000000000 ) ) ;
#10432=CARTESIAN_POINT ( 'NONE',  ( 72.18398860626899705, 28.73617430169837661, 5.000000000000000000 ) ) ;
#10433=DIRECTION ( 'NONE',  ( -0.000000000000000000, -0.3543493200069152693, 0.9351131265310292928 ) ) ;
#10434=CARTESIAN_POINT ( 'NONE',  ( 9.328169399223474656, 11.25929247661560595, 4.000000000000000000 ) ) ;
#10435=CARTESIAN_POINT ( 'NONE',  ( 17.53839644629417904, -9.740707523384184441, 17.74957260769615175 ) ) ;
#10436=DIRECTION ( 'NONE',  ( 0.7071067811865487940, 0.7071067811865463515, 0.000000000000000000 ) ) ;
#10437=ORIENTED_EDGE ( 'NONE', *, *, #68622, .F. ) ;
#10438=VERTEX_POINT ( 'NONE', #58894 ) ;
#10439=PLANE ( 'NONE',  #21790 ) ;
#10441=EDGE_LOOP ( 'NONE', ( #17108, #137049, #40856, #114312 ) ) ;
#10442=ORIENTED_EDGE ( 'NONE', *, *, #71252, .F. ) ;
#10443=EDGE_CURVE ( 'NONE', #75102, #60630, #48676, .T. ) ;
#10444=EDGE_CURVE ( 'NONE', #32455, #36309, #114620, .T. ) ;
#10446=VERTEX_POINT ( 'NONE', #71878 ) ;
#10447=CARTESIAN_POINT ( 'NONE',  ( -21.70710678118638981, 17.25929247661554911, 5.000000000000000000 ) ) ;
#10448=DIRECTION ( 'NONE',  ( -0.7071067811865487940, 0.7071067811865463515, -0.000000000000000000 ) ) ;
#10451=ADVANCED_FACE ( 'NONE', ( #15998 ), #26213, .F. ) ;
#10452=VERTEX_POINT ( 'NONE', #94303 ) ;
#10453=DIRECTION ( 'NONE',  ( -0.7071067811865486830, -0.7071067811865464625, 0.000000000000000000 ) ) ;
#10454=ORIENTED_EDGE ( 'NONE', *, *, #5562, .F. ) ;
#10455=LINE ( 'NONE', #33682, #4758 ) ;
#10456=CARTESIAN_POINT ( 'NONE',  ( 30.18398860626900060, 28.73617430169808173, 5.000000000000000000 ) ) ;
#10457=EDGE_CURVE ( 'NONE', #140051, #124154, #83450, .T. ) ;
#10458=CARTESIAN_POINT ( 'NONE',  ( 22.49999999999984013, 1.030536316426532872, -5.498701923753849918 ) ) ;
#10459=ORIENTED_EDGE ( 'NONE', *, *, #41042, .T. ) ;
#10460=ORIENTED_EDGE ( 'NONE', *, *, #128798, .T. ) ;
#10463=LINE ( 'NONE', #85173, #47120 ) ;
#10464=VERTEX_POINT ( 'NONE', #61712 ) ;
#10465=FACE_OUTER_BOUND ( 'NONE', #52489, .T. ) ;
#10466=ORIENTED_EDGE ( 'NONE', *, *, #24952, .F. ) ;
#10467=ORIENTED_EDGE ( 'NONE', *, *, #10741, .T. ) ;
#10468=LINE ( 'NONE', #64170, #95729 ) ;
#10469=LINE ( 'NONE', #17256, #41768 ) ;
#10472=CARTESIAN_POINT ( 'NONE',  ( -51.48921356237309510, -27.52281430457091460, 5.000000000000000000 ) ) ;
#10474=CARTESIAN_POINT ( 'NONE',  ( 0.4892135623730947680, -27.52281430457055578, 5.000000000000000000 ) ) ;
#10476=VERTEX_POINT ( 'NONE', #28356 ) ;
#10478=EDGE_CURVE ( 'NONE', #31980, #69883, #31123, .T. ) ;
#10479=ORIENTED_EDGE ( 'NONE', *, *, #109268, .F. ) ;
#10480=CARTESIAN_POINT ( 'NONE',  ( -0.1804868739969447966, -22.22500000000000142, 18.16599484154716393 ) ) ;
#10481=EDGE_CURVE ( 'NONE', #109128, #124649, #3691, .T. ) ;
#10482=CARTESIAN_POINT ( 'NONE',  ( 24.24169458425172508, 0.7592924766157138627, 14.37146558664977114 ) ) ;
#10483=AXIS2_PLACEMENT_3D ( 'NONE', #5375, #138790, #107559 ) ;
#10484=CARTESIAN_POINT ( 'NONE',  ( 50.99451991528749062, 28.92564299267973738, 4.000000000000000000 ) ) ;
#10486=PLANE ( 'NONE',  #25198 ) ;
#10487=DIRECTION ( 'NONE',  ( -0.000000000000000000, 0.3543493200069153248, 0.9351131265310292928 ) ) ;
#10489=EDGE_LOOP ( 'NONE', ( #142556, #33169, #22017, #66303 ) ) ;
#10490=VECTOR ( 'NONE', #110578, 1000.000000000000000 ) ;
#10491=ORIENTED_EDGE ( 'NONE', *, *, #49754, .F. ) ;
#10493=CARTESIAN_POINT ( 'NONE',  ( -29.99999999999977973, 5.587461875839189851, 4.000000000000000000 ) ) ;
#10497=CARTESIAN_POINT ( 'NONE',  ( 22.89835756248665888, 7.738675393078206177, 4.667276354320995857 ) ) ;
#10499=FACE_OUTER_BOUND ( 'NONE', #66353, .T. ) ;
#10500=AXIS2_PLACEMENT_3D ( 'NONE', #4946, #28184, #6366 ) ;
#10501=CARTESIAN_POINT ( 'NONE',  ( 36.48921356237310221, -27.52281430457080802, 5.000000000000000000 ) ) ;
#10503=ORIENTED_EDGE ( 'NONE', *, *, #49153, .T. ) ;
#10505=ORIENTED_EDGE ( 'NONE', *, *, #52305, .T. ) ;
#10506=DIRECTION ( 'NONE',  ( 0.7071067811865487940, -0.7071067811865463515, 0.000000000000000000 ) ) ;
#10507=DIRECTION ( 'NONE',  ( 0.7071067811865487940, -0.7071067811865463515, 0.000000000000000000 ) ) ;
#10508=CARTESIAN_POINT ( 'NONE',  ( 34.92499999999998295, -10.29806943317891310, 4.500000000000000888 ) ) ;
#10509=CARTESIAN_POINT ( 'NONE',  ( 7.499999999999945821, -15.29013452822854013, 0.3645803511610531400 ) ) ;
#10510=DIRECTION ( 'NONE',  ( 0.7071067811865486830, -0.7071067811865464625, -0.000000000000000000 ) ) ;
#10511=LINE ( 'NONE', #43890, #60286 ) ;
#10513=ORIENTED_EDGE ( 'NONE', *, *, #40898, .F. ) ;
#10514=ORIENTED_EDGE ( 'NONE', *, *, #7805, .T. ) ;
#10517=CARTESIAN_POINT ( 'NONE',  ( 26.99999999999981171, -16.06887692260765377, 4.000000000000000000 ) ) ;
#10519=FACE_OUTER_BOUND ( 'NONE', #56120, .T. ) ;
#10521=VECTOR ( 'NONE', #55150, 1000.000000000000000 ) ;
#10526=FACE_OUTER_BOUND ( 'NONE', #100809, .T. ) ;
#10527=EDGE_CURVE ( 'NONE', #126051, #90340, #92151, .T. ) ;
#10528=CARTESIAN_POINT ( 'NONE',  ( -0.7586007421979610310, 21.72500000000000853, 5.000000000000000000 ) ) ;
#10529=FACE_OUTER_BOUND ( 'NONE', #62223, .T. ) ;
#10530=AXIS2_PLACEMENT_3D ( 'NONE', #88097, #130907, #96093 ) ;
#10531=ORIENTED_EDGE ( 'NONE', *, *, #138838, .F. ) ;
#10533=VERTEX_POINT ( 'NONE', #137111 ) ;
#10536=ORIENTED_EDGE ( 'NONE', *, *, #26376, .F. ) ;
#10537=DIRECTION ( 'NONE',  ( -0.7071067811865487940, 0.7071067811865463515, 0.000000000000000000 ) ) ;
#10538=LINE ( 'NONE', #76562, #45251 ) ;
#10539=LINE ( 'NONE', #64238, #51204 ) ;
#10540=CARTESIAN_POINT ( 'NONE',  ( -42.48921356237308800, -27.52281430457085065, 5.000000000000000000 ) ) ;
#10541=EDGE_CURVE ( 'NONE', #100628, #10464, #125531, .T. ) ;
#10542=CARTESIAN_POINT ( 'NONE',  ( 16.17183060077635659, -8.240707523384191546, 4.000000000000000000 ) ) ;
#10546=EDGE_CURVE ( 'NONE', #119594, #104026, #129789, .T. ) ;
#10547=DIRECTION ( 'NONE',  ( -0.7071067811865486830, -0.7071067811865464625, 0.000000000000000000 ) ) ;
#10548=CARTESIAN_POINT ( 'NONE',  ( 2.206660635421510808, 21.75929247661549937, 4.998822639870701856 ) ) ;
#10549=LINE ( 'NONE', #30175, #79550 ) ;
#10550=CARTESIAN_POINT ( 'NONE',  ( 23.99451991528749062, 28.92564299267954908, 4.000000000000000000 ) ) ;
#10555=EDGE_CURVE ( 'NONE', #22333, #126257, #117464, .T. ) ;
#10556=DIRECTION ( 'NONE',  ( -0.7071067811865487940, 0.7071067811865463515, 0.000000000000000000 ) ) ;
#10558=DIRECTION ( 'NONE',  ( 1.000000000000000000, 0.000000000000000000, 0.000000000000000000 ) ) ;
#10559=CARTESIAN_POINT ( 'NONE',  ( -54.29974487139159578, -27.71228299555243879, 4.000000000000000000 ) ) ;
#10560=EDGE_LOOP ( 'NONE', ( #80056, #63729, #50043 ) ) ;
#10561=ORIENTED_EDGE ( 'NONE', *, *, #99922, .T. ) ;
#10562=DIRECTION ( 'NONE',  ( 0.7071067811865487940, 0.7071067811865463515, 0.000000000000000000 ) ) ;
#10564=EDGE_CURVE ( 'NONE', #92065, #115116, #7992, .T. ) ;
#10565=EDGE_LOOP ( 'NONE', ( #4504, #12413, #117626, #2283 ) ) ;
#10566=PLANE ( 'NONE',  #125301 ) ;
#10567=LINE ( 'NONE', #30195, #68717 ) ;
#10568=PLANE ( 'NONE',  #60914 ) ;
#10569=EDGE_CURVE ( 'NONE', #19998, #51146, #142127, .T. ) ;
#10571=PLANE ( 'NONE',  #133350 ) ;
#10572=CARTESIAN_POINT ( 'NONE',  ( -30.81246187583926144, -22.22500000000000142, 4.000000000000000000 ) ) ;
#10573=LINE ( 'NONE', #99018, #25806 ) ;
#10574=CARTESIAN_POINT ( 'NONE',  ( 18.79996877983152004, 8.259292476615627265, 16.85664084051836653 ) ) ;
#10575=ADVANCED_FACE ( 'NONE', ( #63148 ), #10149, .F. ) ;
#10576=CARTESIAN_POINT ( 'NONE',  ( -2.004924772211924555, -5.240707523384228850, 12.38332538355496659 ) ) ;
#10577=LINE ( 'NONE', #122200, #14165 ) ;
#10578=VECTOR ( 'NONE', #139878, 1000.000000000000000 ) ;
#10579=ORIENTED_EDGE ( 'NONE', *, *, #31781, .T. ) ;
#10580=EDGE_LOOP ( 'NONE', ( #64730, #52049, #42568, #121371 ) ) ;
#10582=EDGE_LOOP ( 'NONE', ( #101397, #38925, #88341, #19055, #102491, #97567, #29044, #141985, #116303, #17522, #16778, #44898, #44800, #123154, #34916, #94424, #27459, #87782, #127810, #43765, #25069, #120980, #75999, #72239, #43384, #5614, #93405, #82117, #142793, #74385, #99692, #19701, #103530, #113281, #11066, #111155, #129531, #46274, #5459, #92133, #13474, #85217, #58092, #124606, #25024, #75160, #47981, #72176, #58743, #41887, #67165, #47928, #116733, #55917, #68212, #129910, #119038, #39495, #51690, #76774, #7472, #11734, #68497, #137032, #9127, #129493, #107767, #105785, #30850, #52116, #64340, #117701, #11095, #26862, #101731, #34594, #46324, #141723, #22457, #44051, #34386, #34712, #20469, #15879, #49036, #54406 ) ) ;
#10583=VECTOR ( 'NONE', #94198, 1000.000000000000000 ) ;
#10585=EDGE_CURVE ( 'NONE', #57697, #134155, #29751, .T. ) ;
#10587=( BOUNDED_CURVE ( )  B_SPLINE_CURVE ( 3, ( #38517, #28363, #82741, #117470 ),
 .UNSPECIFIED., .F., .F. ) 
 B_SPLINE_CURVE_WITH_KNOTS ( ( 4, 4 ),
 ( 4.350170835173026163, 4.500739107949217832 ),
 .UNSPECIFIED. ) 
 CURVE ( )  GEOMETRIC_REPRESENTATION_ITEM ( )  RATIONAL_B_SPLINE_CURVE ( ( 1.000000000000000000, 0.9981116584018955296, 0.9981116584018955296, 1.000000000000000000 ) ) 
 REPRESENTATION_ITEM ( '' )  );
#10588=DIRECTION ( 'NONE',  ( -0.7071067811865487940, 0.7071067811865463515, -0.000000000000000000 ) ) ;
#10589=EDGE_CURVE ( 'NONE', #19670, #391, #8675, .T. ) ;
#10590=EDGE_CURVE ( 'NONE', #100722, #20115, #42813, .T. ) ;
#10591=DIRECTION ( 'NONE',  ( 0.7071067811865487940, 0.7071067811865463515, 0.000000000000000000 ) ) ;
#10592=ORIENTED_EDGE ( 'NONE', *, *, #62319, .T. ) ;
#10594=DIRECTION ( 'NONE',  ( 0.7071067811865486830, 0.7071067811865464625, 0.000000000000000000 ) ) ;
#10597=DIRECTION ( 'NONE',  ( -0.7071067811865486830, -0.7071067811865464625, 0.000000000000000000 ) ) ;
#10599=FACE_OUTER_BOUND ( 'NONE', #16902, .T. ) ;
#10603=CARTESIAN_POINT ( 'NONE',  ( 29.99999999999979750, 14.87792677143811737, -11.06722581663433225 ) ) ;
#10604=DIRECTION ( 'NONE',  ( 1.000000000000000000, 0.000000000000000000, 0.000000000000000000 ) ) ;
#10606=ORIENTED_EDGE ( 'NONE', *, *, #125426, .T. ) ;
#10607=EDGE_CURVE ( 'NONE', #42048, #49753, #31212, .T. ) ;
#10609=ORIENTED_EDGE ( 'NONE', *, *, #91714, .T. ) ;
#10611=ORIENTED_EDGE ( 'NONE', *, *, #132692, .F. ) ;
#10612=VECTOR ( 'NONE', #46264, 999.9999999999998863 ) ;
#10613=DIRECTION ( 'NONE',  ( 0.7071067811865487940, 0.7071067811865463515, -0.000000000000000000 ) ) ;
#10617=LINE ( 'NONE', #54884, #3119 ) ;
#10619=EDGE_CURVE ( 'NONE', #86643, #114851, #87005, .T. ) ;
#10621=ORIENTED_EDGE ( 'NONE', *, *, #136431, .T. ) ;
#10622=LINE ( 'NONE', #132472, #111178 ) ;
#10623=AXIS2_PLACEMENT_3D ( 'NONE', #1412, #53704, #100759 ) ;
#10624=ADVANCED_FACE ( 'NONE', ( #62420 ), #42100, .T. ) ;
#10625=DIRECTION ( 'NONE',  ( -0.7071067811865487940, 0.7071067811865463515, 0.000000000000000000 ) ) ;
#10627=CARTESIAN_POINT ( 'NONE',  ( 12.29974487139158512, -27.71228299555214747, 4.000000000000000000 ) ) ;
#10628=ORIENTED_EDGE ( 'NONE', *, *, #19186, .T. ) ;
#10629=CARTESIAN_POINT ( 'NONE',  ( 34.92499999999998295, 1.800094516027155755, 4.759050581649325373 ) ) ;
#10631=ORIENTED_EDGE ( 'NONE', *, *, #105264, .F. ) ;
#10635=DIRECTION ( 'NONE',  ( 0.7071067811865486830, -0.7071067811865464625, -0.000000000000000000 ) ) ;
#10636=PLANE ( 'NONE',  #108777 ) ;
#10637=ORIENTED_EDGE ( 'NONE', *, *, #56706, .F. ) ;
#10638=PLANE ( 'NONE',  #132192 ) ;
#10640=EDGE_CURVE ( 'NONE', #57341, #46950, #109472, .T. ) ;
#10641=ADVANCED_FACE ( 'NONE', ( #74732 ), #130533, .F. ) ;
#10643=CARTESIAN_POINT ( 'NONE',  ( 33.18398860626899705, 28.73617430169810305, 5.000000000000000000 ) ) ;
#10644=PLANE ( 'NONE',  #43732 ) ;
#10646=VERTEX_POINT ( 'NONE', #53688 ) ;
#10650=DIRECTION ( 'NONE',  ( 1.000000000000000000, 0.000000000000000000, 0.000000000000000000 ) ) ;
#10651=AXIS2_PLACEMENT_3D ( 'NONE', #49092, #38907, #82420 ) ;
#10652=PLANE ( 'NONE',  #70588 ) ;
#10653=DIRECTION ( 'NONE',  ( -0.7071067811865486830, 0.7071067811865464625, 0.000000000000000000 ) ) ;
#10656=DIRECTION ( 'NONE',  ( 0.7071067811865486830, -0.7071067811865464625, -0.000000000000000000 ) ) ;
#10657=LINE ( 'NONE', #99093, #115984 ) ;
#10658=ORIENTED_EDGE ( 'NONE', *, *, #8135, .T. ) ;
#10659=CARTESIAN_POINT ( 'NONE',  ( 42.48921356237308800, -27.52281430457085065, 5.000000000000000000 ) ) ;
#10660=ORIENTED_EDGE ( 'NONE', *, *, #130402, .F. ) ;
#10662=VERTEX_POINT ( 'NONE', #118911 ) ;
#10663=LINE ( 'NONE', #44808, #131641 ) ;
#10664=DIRECTION ( 'NONE',  ( -0.000000000000000000, 0.3543493200069153248, 0.9351131265310292928 ) ) ;
#10665=ORIENTED_EDGE ( 'NONE', *, *, #133532, .T. ) ;
#10666=LINE ( 'NONE', #19431, #79355 ) ;
#10667=ORIENTED_EDGE ( 'NONE', *, *, #77054, .F. ) ;
#10669=VERTEX_POINT ( 'NONE', #63846 ) ;
#10670=DIRECTION ( 'NONE',  ( 0.7071067811865486830, -0.7071067811865464625, -0.000000000000000000 ) ) ;
#10671=EDGE_LOOP ( 'NONE', ( #41784, #69042, #52389, #71759 ) ) ;
#10672=DIRECTION ( 'NONE',  ( -0.7071067811865486830, -0.7071067811865464625, -0.000000000000000000 ) ) ;
#10673=AXIS2_PLACEMENT_3D ( 'NONE', #20594, #121341, #22027 ) ;
#10676=DIRECTION ( 'NONE',  ( -0.000000000000000000, 0.000000000000000000, 1.000000000000000000 ) ) ;
#10677=VECTOR ( 'NONE', #37540, 1000.000000000000000 ) ;
#10678=DIRECTION ( 'NONE',  ( 0.7071067811865487940, 0.7071067811865463515, 0.000000000000000000 ) ) ;
#10680=EDGE_CURVE ( 'NONE', #17012, #88778, #75428, .T. ) ;
#10681=CARTESIAN_POINT ( 'NONE',  ( -31.17183060077625001, 3.759292476615681888, 4.000000000000000000 ) ) ;
#10684=CARTESIAN_POINT ( 'NONE',  ( 18.18398860626898994, 28.73617430169800002, 5.000000000000000000 ) ) ;
#10686=VERTEX_POINT ( 'NONE', #73996 ) ;
#10687=ORIENTED_EDGE ( 'NONE', *, *, #87402, .T. ) ;
#10688=PLANE ( 'NONE',  #86048 ) ;
#10689=EDGE_CURVE ( 'NONE', #62934, #99425, #51542, .T. ) ;
#10690=ORIENTED_EDGE ( 'NONE', *, *, #121366, .T. ) ;
#10691=DIRECTION ( 'NONE',  ( 0.6830127018922181881, 0.6830127018922202975, -0.2588190451025214056 ) ) ;
#10692=CARTESIAN_POINT ( 'NONE',  ( 7.499999999999951150, -7.533600742197665845, 5.000000000000000000 ) ) ;
#10694=ORIENTED_EDGE ( 'NONE', *, *, #86751, .T. ) ;
#10695=DIRECTION ( 'NONE',  ( -0.7071067811865487940, 0.7071067811865463515, -0.000000000000000000 ) ) ;
#10697=EDGE_CURVE ( 'NONE', #126057, #2927, #84864, .T. ) ;
#10699=VECTOR ( 'NONE', #83897, 1000.000000000000227 ) ;
#10700=LINE ( 'NONE', #23001, #108704 ) ;
#10701=ADVANCED_FACE ( 'NONE', ( #44238 ), #22431, .F. ) ;
#10702=EDGE_CURVE ( 'NONE', #131451, #98806, #43502, .T. ) ;
#10703=DIRECTION ( 'NONE',  ( 1.000000000000000000, 0.000000000000000000, 0.000000000000000000 ) ) ;
#10704=CARTESIAN_POINT ( 'NONE',  ( 19.49999999999985789, 10.94296225409028089, -9.576120664313208408 ) ) ;
#10705=ORIENTED_EDGE ( 'NONE', *, *, #60724, .F. ) ;
#10711=CARTESIAN_POINT ( 'NONE',  ( -27.29974487139158512, -27.71228299555225405, 4.000000000000000000 ) ) ;
#10713=EDGE_CURVE ( 'NONE', #98608, #30859, #57987, .T. ) ;
#10714=ORIENTED_EDGE ( 'NONE', *, *, #112411, .F. ) ;
#10715=ADVANCED_FACE ( 'NONE', ( #68163 ), #111620, .T. ) ;
#10716=EDGE_LOOP ( 'NONE', ( #18905, #2605, #127381, #47740 ) ) ;
#10717=ORIENTED_EDGE ( 'NONE', *, *, #49147, .T. ) ;
#10718=VECTOR ( 'NONE', #28245, 1000.000000000000000 ) ;
#10720=ORIENTED_EDGE ( 'NONE', *, *, #130693, .F. ) ;
#10721=EDGE_CURVE ( 'NONE', #19260, #103619, #57264, .T. ) ;
#10723=VECTOR ( 'NONE', #13546, 999.9999999999998863 ) ;
#10724=CARTESIAN_POINT ( 'NONE',  ( -18.18398860626898994, 28.73617430169800002, 5.000000000000000000 ) ) ;
#10725=EDGE_LOOP ( 'NONE', ( #124183, #48643, #59309, #124345 ) ) ;
#10726=DIRECTION ( 'NONE',  ( 0.3543493200069163240, 0.000000000000000000, -0.9351131265310288487 ) ) ;
#10728=EDGE_CURVE ( 'NONE', #25602, #56797, #87722, .T. ) ;
#10730=ORIENTED_EDGE ( 'NONE', *, *, #10721, .F. ) ;
#10731=DIRECTION ( 'NONE',  ( -0.000000000000000000, 0.3543493200069153248, 0.9351131265310292928 ) ) ;
#10733=EDGE_CURVE ( 'NONE', #128903, #76170, #33384, .T. ) ;
#10734=EDGE_LOOP ( 'NONE', ( #50005, #68158, #136901 ) ) ;
#10735=ORIENTED_EDGE ( 'NONE', *, *, #32945, .F. ) ;
#10736=ORIENTED_EDGE ( 'NONE', *, *, #136700, .F. ) ;
#10737=DIRECTION ( 'NONE',  ( 0.7071067811865487940, 0.7071067811865463515, 0.000000000000000000 ) ) ;
#10740=LINE ( 'NONE', #131850, #34947 ) ;
#10741=EDGE_CURVE ( 'NONE', #126742, #29164, #56576, .T. ) ;
#10742=CARTESIAN_POINT ( 'NONE',  ( 18.27825451568562443, 8.259292476615637923, 11.78515199841154448 ) ) ;
#10743=CARTESIAN_POINT ( 'NONE',  ( 18.29974487139159223, -27.71228299555219010, 4.000000000000000000 ) ) ;
#10744=SHAPE_REPRESENTATION_RELATIONSHIP ( 'NONE' , 'NONE' ,  #103311, #34315 ) ;
#10745=ORIENTED_EDGE ( 'NONE', *, *, #113692, .F. ) ;
#10746=( BOUNDED_CURVE ( )  B_SPLINE_CURVE ( 3, ( #99192, #76050, #10061, #86932 ),
 .UNSPECIFIED., .F., .T. ) 
 B_SPLINE_CURVE_WITH_KNOTS ( ( 4, 4 ),
 ( 1.610468072580458099, 1.654543780452488067 ),
 .UNSPECIFIED. ) 
 CURVE ( )  GEOMETRIC_REPRESENTATION_ITEM ( )  RATIONAL_B_SPLINE_CURVE ( ( 1.000000000000000000, 0.9998381175498709528, 0.9998381175498709528, 1.000000000000000000 ) ) 
 REPRESENTATION_ITEM ( '' )  );
#10747=ORIENTED_EDGE ( 'NONE', *, *, #134375, .F. ) ;
#10748=PLANE ( 'NONE',  #29458 ) ;
#10752=CIRCLE ( 'NONE', #50228, 0.5000000000000000000 ) ;
#10755=VERTEX_POINT ( 'NONE', #89157 ) ;
#10756=LINE ( 'NONE', #120966, #18129 ) ;
#10758=EDGE_CURVE ( 'NONE', #1674, #84583, #76882, .T. ) ;
#10759=CARTESIAN_POINT ( 'NONE',  ( 18.18398860626898994, 28.73617430169800002, 5.000000000000000000 ) ) ;
#10760=VECTOR ( 'NONE', #2472, 1000.000000000000000 ) ;
#10761=FACE_OUTER_BOUND ( 'NONE', #117110, .T. ) ;
#10764=ADVANCED_FACE ( 'NONE', ( #55105 ), #13695, .F. ) ;
#10765=DIRECTION ( 'NONE',  ( -0.7071067811865486830, -0.7071067811865464625, 0.000000000000000000 ) ) ;
#10766=VECTOR ( 'NONE', #121837, 1000.000000000000000 ) ;
#10767=ORIENTED_EDGE ( 'NONE', *, *, #51040, .T. ) ;
#10769=EDGE_LOOP ( 'NONE', ( #67088, #124146, #100815, #127063, #5462 ) ) ;
#10771=ORIENTED_EDGE ( 'NONE', *, *, #72463, .F. ) ;
#10772=DIRECTION ( 'NONE',  ( -0.6830127018922181881, 0.6830127018922202975, -0.2588190451025214056 ) ) ;
#10773=ORIENTED_EDGE ( 'NONE', *, *, #18277, .F. ) ;
#10774=ORIENTED_EDGE ( 'NONE', *, *, #35599, .F. ) ;
#10776=VECTOR ( 'NONE', #129918, 1000.000000000000000 ) ;
#10777=PLANE ( 'NONE',  #83629 ) ;
#10778=CARTESIAN_POINT ( 'NONE',  ( 20.29298673570680123, -21.74070752338406720, 4.999753212805221558 ) ) ;
#10779=FACE_OUTER_BOUND ( 'NONE', #122890, .T. ) ;
#10781=DIRECTION ( 'NONE',  ( -0.7071067811865486830, -0.7071067811865464625, -0.000000000000000000 ) ) ;
#10782=EDGE_CURVE ( 'NONE', #47934, #46563, #132697, .T. ) ;
#10784=DIRECTION ( 'NONE',  ( -0.7071067811865487940, 0.7071067811865463515, 0.000000000000000000 ) ) ;
#10786=DIRECTION ( 'NONE',  ( -0.6830127018922180770, -0.6830127018922204085, -0.2588190451025213501 ) ) ;
#10787=CARTESIAN_POINT ( 'NONE',  ( -28.49999999999980105, 8.900465351122127444, -2.516491619111447253 ) ) ;
#10789=DIRECTION ( 'NONE',  ( -0.7071067811865486830, -0.7071067811865464625, 0.000000000000000000 ) ) ;
#10790=CARTESIAN_POINT ( 'NONE',  ( 11.99451991528749417, 28.92564299267946382, 4.000000000000000000 ) ) ;
#10792=ORIENTED_EDGE ( 'NONE', *, *, #72823, .T. ) ;
#10793=ORIENTED_EDGE ( 'NONE', *, *, #86774, .T. ) ;
#10794=ORIENTED_EDGE ( 'NONE', *, *, #124173, .F. ) ;
#10796=VERTEX_POINT ( 'NONE', #1389 ) ;
#10797=EDGE_LOOP ( 'NONE', ( #36828, #40489, #4231, #40619 ) ) ;
#10799=LINE ( 'NONE', #102143, #20066 ) ;
#10802=PLANE ( 'NONE',  #40310 ) ;
#10803=DIRECTION ( 'NONE',  ( -0.000000000000000000, 0.3543493200069153248, 0.9351131265310292928 ) ) ;
#10804=EDGE_CURVE ( 'NONE', #89814, #130555, #45678, .T. ) ;
#10805=ORIENTED_EDGE ( 'NONE', *, *, #123402, .T. ) ;
#10806=LINE ( 'NONE', #133347, #78908 ) ;
#10807=ORIENTED_EDGE ( 'NONE', *, *, #18970, .T. ) ;
#10809=VECTOR ( 'NONE', #2915, 1000.000000000000227 ) ;
#10810=DIRECTION ( 'NONE',  ( 1.000000000000000000, 0.000000000000000000, 0.000000000000000000 ) ) ;
#10811=EDGE_CURVE ( 'NONE', #33166, #41654, #10839, .T. ) ;
#10812=AXIS2_PLACEMENT_3D ( 'NONE', #137697, #49972, #62271 ) ;
#10814=VERTEX_POINT ( 'NONE', #99279 ) ;
#10817=LINE ( 'NONE', #54387, #90729 ) ;
#10819=ORIENTED_EDGE ( 'NONE', *, *, #63338, .F. ) ;
#10821=EDGE_LOOP ( 'NONE', ( #21799, #47488, #52267 ) ) ;
#10823=CARTESIAN_POINT ( 'NONE',  ( 18.29177708983036155, -15.74070752338412049, 19.73771281079102025 ) ) ;
#10824=DIRECTION ( 'NONE',  ( 1.000000000000000000, 0.000000000000000000, 0.000000000000000000 ) ) ;
#10825=DIRECTION ( 'NONE',  ( 0.7071067811865487940, 0.7071067811865463515, 0.000000000000000000 ) ) ;
#10827=EDGE_LOOP ( 'NONE', ( #122460, #64236, #22015, #132483 ) ) ;
#10828=LINE ( 'NONE', #84851, #64625 ) ;
#10829=ADVANCED_FACE ( 'NONE', ( #143525 ), #100038, .F. ) ;
#10830=FACE_OUTER_BOUND ( 'NONE', #70848, .T. ) ;
#10831=VERTEX_POINT ( 'NONE', #41015 ) ;
#10832=FACE_OUTER_BOUND ( 'NONE', #58942, .T. ) ;
#10833=DIRECTION ( 'NONE',  ( -0.6830127018922181881, 0.6830127018922202975, -0.2588190451025214056 ) ) ;
#10834=ORIENTED_EDGE ( 'NONE', *, *, #52564, .T. ) ;
#10835=DIRECTION ( 'NONE',  ( 0.3543493200069162685, -0.000000000000000000, -0.9351131265310288487 ) ) ;
#10836=VERTEX_POINT ( 'NONE', #62792 ) ;
#10838=EDGE_CURVE ( 'NONE', #70323, #67112, #135524, .T. ) ;
#10839=LINE ( 'NONE', #23141, #72484 ) ;
#10840=CARTESIAN_POINT ( 'NONE',  ( 34.42499999999998295, -21.02281430457037814, 5.000000000000000000 ) ) ;
#10841=AXIS2_PLACEMENT_3D ( 'NONE', #21166, #87853, #42232 ) ;
#10842=ORIENTED_EDGE ( 'NONE', *, *, #143170, .F. ) ;
#10843=CARTESIAN_POINT ( 'NONE',  ( -26.99999999999981526, 14.96639925780211122, 5.000000000000000000 ) ) ;
#10844=DIRECTION ( 'NONE',  ( -0.7071067811865486830, 0.7071067811865464625, 0.000000000000000000 ) ) ;
#10845=VECTOR ( 'NONE', #45938, 1000.000000000000000 ) ;
#10846=LINE ( 'NONE', #88461, #78527 ) ;
#10847=DIRECTION ( 'NONE',  ( 0.6830127018922181881, 0.6830127018922202975, -0.2588190451025214056 ) ) ;
#10849=DIRECTION ( 'NONE',  ( -0.000000000000000000, 0.3543493200069152138, -0.9351131265310292928 ) ) ;
#10850=CARTESIAN_POINT ( 'NONE',  ( 31.49999999999979039, 9.052185695429082912, 5.000000000000000000 ) ) ;
#10851=DIRECTION ( 'NONE',  ( -0.7071067811865486830, -0.7071067811865464625, 0.000000000000000000 ) ) ;
#10852=CARTESIAN_POINT ( 'NONE',  ( -3.121473163371450532, -20.24070752338407431, 7.412974875817798903 ) ) ;
#10853=CARTESIAN_POINT ( 'NONE',  ( -11.51078643762690490, -27.52281430457047406, 5.000000000000000000 ) ) ;
#10854=CARTESIAN_POINT ( 'NONE',  ( 12.18398860626900060, 28.73617430169795739, 5.000000000000000000 ) ) ;
#10855=CARTESIAN_POINT ( 'NONE',  ( -8.510786437626906675, -27.52281430457049183, 5.000000000000000000 ) ) ;
#10856=DIRECTION ( 'NONE',  ( -0.000000000000000000, -1.000000000000000000, -0.000000000000000000 ) ) ;
#10857=ORIENTED_EDGE ( 'NONE', *, *, #89335, .F. ) ;
#10858=ORIENTED_EDGE ( 'NONE', *, *, #13481, .T. ) ;
#10860=ORIENTED_EDGE ( 'NONE', *, *, #113036, .T. ) ;
#10861=EDGE_LOOP ( 'NONE', ( #104495, #39016, #17230, #63991 ) ) ;
#10862=VERTEX_POINT ( 'NONE', #2839 ) ;
#10863=VECTOR ( 'NONE', #1580, 1000.000000000000227 ) ;
#10866=ORIENTED_EDGE ( 'NONE', *, *, #43496, .T. ) ;
#10869=LINE ( 'NONE', #55138, #122797 ) ;
#10870=AXIS2_PLACEMENT_3D ( 'NONE', #135607, #59491, #80523 ) ;
#10871=CARTESIAN_POINT ( 'NONE',  ( -15.75860074219783513, 21.72499999999999432, 5.000000000000000000 ) ) ;
#10872=ORIENTED_EDGE ( 'NONE', *, *, #82734, .T. ) ;
#10873=EDGE_CURVE ( 'NONE', #91527, #75052, #81881, .T. ) ;
#10874=PLANE ( 'NONE',  #37240 ) ;
#10875=FACE_OUTER_BOUND ( 'NONE', #96640, .T. ) ;
#10876=CARTESIAN_POINT ( 'NONE',  ( -33.70710678118631165, 5.259292476615663681, 5.000000000000000000 ) ) ;
#10877=DIRECTION ( 'NONE',  ( -0.7071067811865487940, 0.7071067811865463515, 0.000000000000000000 ) ) ;
#10878=CARTESIAN_POINT ( 'NONE',  ( -47.99451991528749062, 28.92564299267971251, 4.000000000000000000 ) ) ;
#10879=CARTESIAN_POINT ( 'NONE',  ( 33.29974487139158867, -27.71228299555229313, 4.000000000000000000 ) ) ;
#10880=CARTESIAN_POINT ( 'NONE',  ( -20.58838509405153872, 22.22500000000000142, 4.777194822843816802 ) ) ;
#10881=EDGE_CURVE ( 'NONE', #46464, #33991, #129439, .T. ) ;
#10882=ADVANCED_FACE ( 'NONE', ( #58722 ), #126074, .F. ) ;
#10883=ORIENTED_EDGE ( 'NONE', *, *, #106107, .F. ) ;
#10884=ORIENTED_EDGE ( 'NONE', *, *, #95378, .F. ) ;
#10887=AXIS2_PLACEMENT_3D ( 'NONE', #41446, #129894, #87108 ) ;
#10888=VERTEX_POINT ( 'NONE', #80435 ) ;
#10889=DIRECTION ( 'NONE',  ( -0.6830127018922180770, -0.6830127018922204085, -0.2588190451025213501 ) ) ;
#10890=EDGE_CURVE ( 'NONE', #58827, #9095, #36207, .T. ) ;
#10891=LINE ( 'NONE', #109524, #138180 ) ;
#10892=EDGE_CURVE ( 'NONE', #35612, #40957, #125746, .T. ) ;
#10894=DIRECTION ( 'NONE',  ( 0.3543493200069162685, -0.000000000000000000, -0.9351131265310288487 ) ) ;
#10895=DIRECTION ( 'NONE',  ( 0.3543493200069162685, -0.000000000000000000, -0.9351131265310288487 ) ) ;
#10896=ADVANCED_FACE ( 'NONE', ( #114454 ), #3525, .F. ) ;
#10898=VECTOR ( 'NONE', #48973, 1000.000000000000000 ) ;
#10900=ORIENTED_EDGE ( 'NONE', *, *, #57447, .T. ) ;
#10901=DIRECTION ( 'NONE',  ( -0.6830127018922180770, -0.6830127018922204085, -0.2588190451025213501 ) ) ;
#10903=EDGE_CURVE ( 'NONE', #104204, #60317, #19264, .T. ) ;
#10904=ORIENTED_EDGE ( 'NONE', *, *, #112761, .T. ) ;
#10905=ORIENTED_EDGE ( 'NONE', *, *, #84266, .F. ) ;
#10910=LINE ( 'NONE', #45053, #31652 ) ;
#10911=CARTESIAN_POINT ( 'NONE',  ( -20.99999999999984723, 8.966399257802164513, 5.000000000000000000 ) ) ;
#10912=ADVANCED_FACE ( 'NONE', ( #27433 ), #106973, .T. ) ;
#10913=AXIS2_PLACEMENT_3D ( 'NONE', #36618, #72159, #117037 ) ;
#10914=VECTOR ( 'NONE', #32934, 1000.000000000000000 ) ;
#10915=AXIS2_PLACEMENT_3D ( 'NONE', #47361, #36428, #5184 ) ;
#10917=ORIENTED_EDGE ( 'NONE', *, *, #3403, .F. ) ;
#10918=LINE ( 'NONE', #55184, #66432 ) ;
#10919=EDGE_LOOP ( 'NONE', ( #17575, #84950, #109361 ) ) ;
#10920=ORIENTED_EDGE ( 'NONE', *, *, #62506, .F. ) ;
#10921=AXIS2_PLACEMENT_3D ( 'NONE', #133798, #100459, #45390 ) ;
#10922=EDGE_LOOP ( 'NONE', ( #79873, #71519, #18855, #56172 ) ) ;
#10923=CARTESIAN_POINT ( 'NONE',  ( -1.171830600776462061, -20.24070752338407786, 4.000000000000000000 ) ) ;
#10924=ORIENTED_EDGE ( 'NONE', *, *, #129152, .F. ) ;
#10925=CARTESIAN_POINT ( 'NONE',  ( -25.01899999999999835, 3.174999999999998046, 1.444000000000000394 ) ) ;
#10926=EDGE_CURVE ( 'NONE', #120446, #90697, #136211, .T. ) ;
#10927=DIRECTION ( 'NONE',  ( 0.7071067811865487940, -0.7071067811865463515, 0.000000000000000000 ) ) ;
#10929=CARTESIAN_POINT ( 'NONE',  ( -72.18398860626899705, 28.73617430169837661, 5.000000000000000000 ) ) ;
#10930=FACE_BOUND ( 'NONE', #17757, .T. ) ;
#10932=DIRECTION ( 'NONE',  ( 0.7071067811865487940, -0.7071067811865463515, 0.000000000000000000 ) ) ;
#10933=LINE ( 'NONE', #44342, #53882 ) ;
#10934=FACE_OUTER_BOUND ( 'NONE', #14311, .T. ) ;
#10935=VERTEX_POINT ( 'NONE', #82557 ) ;
#10936=DIRECTION ( 'NONE',  ( -0.7071067811865486830, -0.7071067811865464625, -0.000000000000000000 ) ) ;
#10937=ORIENTED_EDGE ( 'NONE', *, *, #95403, .T. ) ;
#10938=VECTOR ( 'NONE', #40282, 1000.000000000000000 ) ;
#10939=EDGE_LOOP ( 'NONE', ( #14303, #113302, #22318, #99897 ) ) ;
#10941=EDGE_CURVE ( 'NONE', #140728, #85524, #7652, .T. ) ;
#10942=EDGE_LOOP ( 'NONE', ( #83129, #135686, #85684, #128238 ) ) ;
#10945=ORIENTED_EDGE ( 'NONE', *, *, #118311, .T. ) ;
#10946=LINE ( 'NONE', #130650, #111203 ) ;
#10947=EDGE_CURVE ( 'NONE', #94548, #32452, #136932, .T. ) ;
#10948=LINE ( 'NONE', #55943, #132111 ) ;
#10949=ORIENTED_EDGE ( 'NONE', *, *, #30753, .F. ) ;
#10950=CARTESIAN_POINT ( 'NONE',  ( -11.99999999999991296, 19.93112307739198386, 4.000000000000000000 ) ) ;
#10951=DIRECTION ( 'NONE',  ( 0.7071067811865486830, -0.7071067811865464625, -0.000000000000000000 ) ) ;
#10952=AXIS2_PLACEMENT_3D ( 'NONE', #120759, #52649, #131660 ) ;
#10953=LINE ( 'NONE', #13108, #22364 ) ;
#10954=CARTESIAN_POINT ( 'NONE',  ( 27.32816939922333432, 17.25929247661553489, 4.000000000000000000 ) ) ;
#10955=DIRECTION ( 'NONE',  ( 0.7071067811865486830, -0.7071067811865464625, -0.000000000000000000 ) ) ;
#10957=CARTESIAN_POINT ( 'NONE',  ( -39.29974487139159578, -27.71228299555233576, 4.000000000000000000 ) ) ;
#10958=ORIENTED_EDGE ( 'NONE', *, *, #16461, .T. ) ;
#10959=VECTOR ( 'NONE', #131083, 1000.000000000000000 ) ;
#10960=ORIENTED_EDGE ( 'NONE', *, *, #96802, .T. ) ;
#10961=ORIENTED_EDGE ( 'NONE', *, *, #101657, .T. ) ;
#10962=DIRECTION ( 'NONE',  ( -0.7071067811865487940, 0.7071067811865463515, 0.000000000000000000 ) ) ;
#10963=CARTESIAN_POINT ( 'NONE',  ( 31.82816939922331656, 18.75929247661552779, 4.000000000000000000 ) ) ;
#10965=VERTEX_POINT ( 'NONE', #117823 ) ;
#10967=CARTESIAN_POINT ( 'NONE',  ( -21.18398860626899349, 28.73617430169802134, 5.000000000000000000 ) ) ;
#10968=EDGE_CURVE ( 'NONE', #25822, #93317, #18513, .T. ) ;
#10969=EDGE_CURVE ( 'NONE', #23067, #123360, #140329, .T. ) ;
#10971=ORIENTED_EDGE ( 'NONE', *, *, #86600, .T. ) ;
#10973=LINE ( 'NONE', #55242, #5066 ) ;
#10974=ADVANCED_FACE ( 'NONE', ( #107685 ), #30874, .T. ) ;
#10976=CARTESIAN_POINT ( 'NONE',  ( -28.49999999999980460, 6.431123077392117082, 4.000000000000000000 ) ) ;
#10977=VERTEX_POINT ( 'NONE', #33736 ) ;
#10980=ADVANCED_FACE ( 'NONE', ( #54073 ), #9041, .F. ) ;
#10982=LINE ( 'NONE', #111016, #3271 ) ;
#10983=CARTESIAN_POINT ( 'NONE',  ( 9.411614905948244569, 22.22499999999999787, 4.777194822843815913 ) ) ;
#10984=ORIENTED_EDGE ( 'NONE', *, *, #61384, .F. ) ;
#10986=ORIENTED_EDGE ( 'NONE', *, *, #136603, .T. ) ;
#10987=DIRECTION ( 'NONE',  ( 0.6830127018922181881, 0.6830127018922202975, -0.2588190451025214056 ) ) ;
#10988=DIRECTION ( 'NONE',  ( 0.3543493200069163240, -0.000000000000000000, -0.9351131265310288487 ) ) ;
#10989=LINE ( 'NONE', #12443, #112060 ) ;
#10991=EDGE_CURVE ( 'NONE', #128295, #115416, #77940, .T. ) ;
#10993=EDGE_CURVE ( 'NONE', #91708, #63130, #75103, .T. ) ;
#10995=CARTESIAN_POINT ( 'NONE',  ( 48.48921356237309510, -27.52281430457089328, 5.000000000000000000 ) ) ;
#10996=ORIENTED_EDGE ( 'NONE', *, *, #17068, .F. ) ;
#10998=VECTOR ( 'NONE', #92644, 1000.000000000000000 ) ;
#10999=DIRECTION ( 'NONE',  ( 0.6830127018922181881, 0.6830127018922202975, -0.2588190451025214056 ) ) ;
#11000=ORIENTED_EDGE ( 'NONE', *, *, #47976, .F. ) ;
#11001=AXIS2_PLACEMENT_3D ( 'NONE', #55554, #21490, #141857 ) ;
#11002=LINE ( 'NONE', #79917, #103986 ) ;
#11003=PLANE ( 'NONE',  #30164 ) ;
#11004=ORIENTED_EDGE ( 'NONE', *, *, #80247, .T. ) ;
#11005=EDGE_CURVE ( 'NONE', #124489, #32019, #52596, .T. ) ;
#11009=VECTOR ( 'NONE', #65210, 1000.000000000000000 ) ;
#11012=CARTESIAN_POINT ( 'NONE',  ( 32.67183060077623935, 17.25929247661554200, 4.000000000000000000 ) ) ;
#11013=CARTESIAN_POINT ( 'NONE',  ( -14.67183060077636370, -3.740707523384238176, 4.000000000000000000 ) ) ;
#11014=CARTESIAN_POINT ( 'NONE',  ( -17.99999999999986855, -12.41253812416062985, 4.000000000000000000 ) ) ;
#11015=ORIENTED_EDGE ( 'NONE', *, *, #25652, .T. ) ;
#11016=LINE ( 'NONE', #53871, #20983 ) ;
#11017=DIRECTION ( 'NONE',  ( -0.000000000000000000, 0.000000000000000000, 1.000000000000000000 ) ) ;
#11018=CARTESIAN_POINT ( 'NONE',  ( 2.148183550381434603, 17.25929247661554200, 8.802941693769207987 ) ) ;
#11019=DIRECTION ( 'NONE',  ( -0.000000000000000000, 0.3543493200069153248, 0.9351131265310292928 ) ) ;
#11022=ORIENTED_EDGE ( 'NONE', *, *, #121000, .F. ) ;
#11023=ORIENTED_EDGE ( 'NONE', *, *, #43055, .T. ) ;
#11025=VERTEX_POINT ( 'NONE', #41732 ) ;
#11026=ORIENTED_EDGE ( 'NONE', *, *, #33932, .F. ) ;
#11027=CARTESIAN_POINT ( 'NONE',  ( -14.99999999999989164, -16.06887692260766087, 4.000000000000000000 ) ) ;
#11028=CARTESIAN_POINT ( 'NONE',  ( -33.48921356237309510, -27.52281430457078670, 5.000000000000000000 ) ) ;
#11029=ORIENTED_EDGE ( 'NONE', *, *, #43165, .F. ) ;
#11031=CARTESIAN_POINT ( 'NONE',  ( -74.99451991528749772, 28.92564299267990435, 4.000000000000000000 ) ) ;
#11032=DIRECTION ( 'NONE',  ( 0.7071067811865487940, 0.7071067811865463515, 0.000000000000000000 ) ) ;
#11034=CARTESIAN_POINT ( 'NONE',  ( -4.362461875838996583, 22.22500000000000142, 4.000000000000000000 ) ) ;
#11036=ORIENTED_EDGE ( 'NONE', *, *, #120554, .F. ) ;
#11037=CARTESIAN_POINT ( 'NONE',  ( 14.99999999999990052, -6.033600742197674727, 5.000000000000000000 ) ) ;
#11042=FACE_OUTER_BOUND ( 'NONE', #128508, .T. ) ;
#11043=CARTESIAN_POINT ( 'NONE',  ( 56.99451991528749062, 28.92564299267978001, 4.000000000000000000 ) ) ;
#11044=CARTESIAN_POINT ( 'NONE',  ( 29.99999999999979039, -16.60178936734445898, 0.8616154019348201132 ) ) ;
#11047=EDGE_CURVE ( 'NONE', #98610, #115536, #132345, .T. ) ;
#11050=ORIENTED_EDGE ( 'NONE', *, *, #111323, .T. ) ;
#11052=EDGE_CURVE ( 'NONE', #115757, #81768, #108364, .T. ) ;
#11055=EDGE_CURVE ( 'NONE', #94607, #51968, #11195, .T. ) ;
#11056=CARTESIAN_POINT ( 'NONE',  ( 5.994519915287488843, 28.92564299267942118, 4.000000000000000000 ) ) ;
#11057=VERTEX_POINT ( 'NONE', #32291 ) ;
#11058=EDGE_CURVE ( 'NONE', #99644, #99824, #96772, .T. ) ;
#11059=DIRECTION ( 'NONE',  ( -0.7071067811865486830, -0.7071067811865464625, -0.000000000000000000 ) ) ;
#11060=DIRECTION ( 'NONE',  ( -0.000000000000000000, 0.000000000000000000, 1.000000000000000000 ) ) ;
#11063=EDGE_CURVE ( 'NONE', #125846, #113106, #141026, .T. ) ;
#11065=VERTEX_POINT ( 'NONE', #9803 ) ;
#11066=ORIENTED_EDGE ( 'NONE', *, *, #14501, .F. ) ;
#11067=LINE ( 'NONE', #87243, #128016 ) ;
#11068=CARTESIAN_POINT ( 'NONE',  ( 33.79289321881321939, 3.759292476615678336, 5.000000000000000000 ) ) ;
#11069=CARTESIAN_POINT ( 'NONE',  ( -34.92500000000001137, 15.58119340046981449, 2.482413320905447307 ) ) ;
#11070=EDGE_CURVE ( 'NONE', #125811, #98878, #99662, .T. ) ;
#11071=CARTESIAN_POINT ( 'NONE',  ( -81.48921356237309510, -27.52281430457112066, 5.000000000000000000 ) ) ;
#11072=ORIENTED_EDGE ( 'NONE', *, *, #24523, .T. ) ;
#11073=ADVANCED_FACE ( 'NONE', ( #55475 ), #21412, .F. ) ;
#11074=CARTESIAN_POINT ( 'NONE',  ( 0.000000000000000000, 0.000000000000000000, 5.000000000000000000 ) ) ;
#11078=FACE_OUTER_BOUND ( 'NONE', #4361, .T. ) ;
#11082=ADVANCED_FACE ( 'NONE', ( #109838 ), #53306, .F. ) ;
#11083=ORIENTED_EDGE ( 'NONE', *, *, #89920, .F. ) ;
#11085=CARTESIAN_POINT ( 'NONE',  ( -25.49999999999982236, 0.4311230773921901349, 4.000000000000000000 ) ) ;
#11088=CARTESIAN_POINT ( 'NONE',  ( -32.27718569542918203, -21.72500000000000142, 5.000000000000000000 ) ) ;
#11089=CARTESIAN_POINT ( 'NONE',  ( 19.05000000000000071, 3.174999999999997158, 5.000000000000000000 ) ) ;
#11091=VERTEX_POINT ( 'NONE', #44634 ) ;
#11092=PLANE ( 'NONE',  #35320 ) ;
#11093=ORIENTED_EDGE ( 'NONE', *, *, #70212, .T. ) ;
#11094=CARTESIAN_POINT ( 'NONE',  ( -5.671830600776431197, 2.259292476615694323, 4.000000000000000000 ) ) ;
#11095=ORIENTED_EDGE ( 'NONE', *, *, #124617, .T. ) ;
#11097=FACE_OUTER_BOUND ( 'NONE', #127249, .T. ) ;
#11098=EDGE_CURVE ( 'NONE', #47328, #29533, #75800, .T. ) ;
#11100=LINE ( 'NONE', #109735, #129961 ) ;
#11102=FACE_BOUND ( 'NONE', #45927, .T. ) ;
#11103=FACE_OUTER_BOUND ( 'NONE', #13864, .T. ) ;
#11104=LINE ( 'NONE', #1654, #109106 ) ;
#11105=PLANE ( 'NONE',  #71203 ) ;
#11106=DIRECTION ( 'NONE',  ( 0.3543493200069162685, -0.000000000000000000, -0.9351131265310288487 ) ) ;
#11107=EDGE_LOOP ( 'NONE', ( #28870, #25540, #82963, #128463 ) ) ;
#11108=VECTOR ( 'NONE', #6659, 1000.000000000000000 ) ;
#11109=VECTOR ( 'NONE', #131879, 1000.000000000000000 ) ;
#11110=LINE ( 'NONE', #112607, #136592 ) ;
#11112=VERTEX_POINT ( 'NONE', #48160 ) ;
#11113=VERTEX_POINT ( 'NONE', #36556 ) ;
#11115=ORIENTED_EDGE ( 'NONE', *, *, #90142, .F. ) ;
#11116=LINE ( 'NONE', #98860, #77718 ) ;
#11117=LINE ( 'NONE', #142406, #21176 ) ;
#11119=ORIENTED_EDGE ( 'NONE', *, *, #91714, .F. ) ;
#11120=CARTESIAN_POINT ( 'NONE',  ( 54.29974487139159578, -27.71228299555243879, 4.000000000000000000 ) ) ;
#11121=FACE_OUTER_BOUND ( 'NONE', #104882, .T. ) ;
#11123=FACE_OUTER_BOUND ( 'NONE', #68974, .T. ) ;
#11125=PLANE ( 'NONE',  #139571 ) ;
#11126=DIRECTION ( 'NONE',  ( -0.7071067811865486830, -0.7071067811865464625, -0.000000000000000000 ) ) ;
#11127=VERTEX_POINT ( 'NONE', #136571 ) ;
#11129=FACE_OUTER_BOUND ( 'NONE', #1417, .T. ) ;
#11133=VERTEX_POINT ( 'NONE', #78646 ) ;
#11136=VECTOR ( 'NONE', #66639, 1000.000000000000000 ) ;
#11139=FACE_OUTER_BOUND ( 'NONE', #122062, .T. ) ;
#11142=ORIENTED_EDGE ( 'NONE', *, *, #129727, .F. ) ;
#11143=ORIENTED_EDGE ( 'NONE', *, *, #57313, .T. ) ;
#11145=CARTESIAN_POINT ( 'NONE',  ( -26.99999999999980460, 5.966399257802205369, 5.000000000000000000 ) ) ;
#11146=VECTOR ( 'NONE', #34721, 1000.000000000000000 ) ;
#11147=CARTESIAN_POINT ( 'NONE',  ( 32.99999999999975842, -4.447814304570784749, 5.000000000000000000 ) ) ;
#11149=VERTEX_POINT ( 'NONE', #111245 ) ;
#11150=CARTESIAN_POINT ( 'NONE',  ( -26.29289321881327623, -18.74070752338408852, 5.000000000000000000 ) ) ;
#11151=CARTESIAN_POINT ( 'NONE',  ( 25.11017322888192993, -22.22499999999999787, 4.785647885939354751 ) ) ;
#11153=DIRECTION ( 'NONE',  ( 0.7071067811865487940, -0.7071067811865463515, 0.000000000000000000 ) ) ;
#11154=VERTEX_POINT ( 'NONE', #103233 ) ;
#11156=EDGE_CURVE ( 'NONE', #126185, #16532, #45337, .T. ) ;
#11157=ORIENTED_EDGE ( 'NONE', *, *, #83427, .T. ) ;
#11158=DIRECTION ( 'NONE',  ( 0.7071067811865487940, 0.7071067811865463515, 0.000000000000000000 ) ) ;
#11160=DIRECTION ( 'NONE',  ( 0.7071067811865487940, 0.7071067811865463515, 0.000000000000000000 ) ) ;
#11163=FACE_OUTER_BOUND ( 'NONE', #140533, .T. ) ;
#11164=DIRECTION ( 'NONE',  ( 0.3543493200069162685, -0.000000000000000000, -0.9351131265310288487 ) ) ;
#11165=EDGE_CURVE ( 'NONE', #10977, #95984, #89513, .T. ) ;
#11166=LINE ( 'NONE', #131570, #13544 ) ;
#11167=VERTEX_POINT ( 'NONE', #81529 ) ;
#11169=DIRECTION ( 'NONE',  ( 0.7071067811865487940, 0.7071067811865463515, 0.000000000000000000 ) ) ;
#11170=VERTEX_POINT ( 'NONE', #100406 ) ;
#11171=LINE ( 'NONE', #55448, #42456 ) ;
#11172=CARTESIAN_POINT ( 'NONE',  ( 35.16170612452598476, -6.740707523384216415, 16.75550250614875836 ) ) ;
#11173=LINE ( 'NONE', #45316, #66757 ) ;
#11174=ORIENTED_EDGE ( 'NONE', *, *, #25728, .F. ) ;
#11175=LINE ( 'NONE', #2457, #80893 ) ;
#11176=FACE_OUTER_BOUND ( 'NONE', #89911, .T. ) ;
#11177=CARTESIAN_POINT ( 'NONE',  ( 29.99999999999979394, -16.06887692260766087, 4.000000000000000000 ) ) ;
#11180=LINE ( 'NONE', #34410, #78937 ) ;
#11184=LINE ( 'NONE', #130894, #129253 ) ;
#11186=EDGE_CURVE ( 'NONE', #72863, #133600, #37282, .T. ) ;
#11187=LINE ( 'NONE', #23531, #37143 ) ;
#11188=LINE ( 'NONE', #33730, #55479 ) ;
#11190=AXIS2_PLACEMENT_3D ( 'NONE', #2998, #123394, #13144 ) ;
#11191=CARTESIAN_POINT ( 'NONE',  ( 4.828169399223496860, 15.75929247661555976, 4.000000000000000000 ) ) ;
#11192=EDGE_LOOP ( 'NONE', ( #6135, #103139, #11813, #30520 ) ) ;
#11193=LINE ( 'NONE', #34419, #106640 ) ;
#11194=EDGE_LOOP ( 'NONE', ( #597, #101217, #21221, #118504 ) ) ;
#11195=LINE ( 'NONE', #43173, #68667 ) ;
#11196=DIRECTION ( 'NONE',  ( -0.000000000000000000, 0.3543493200069153248, 0.9351131265310292928 ) ) ;
#11197=AXIS2_PLACEMENT_3D ( 'NONE', #2757, #22344, #78205 ) ;
#11198=VECTOR ( 'NONE', #85526, 1000.000000000000000 ) ;
#11199=VECTOR ( 'NONE', #87100, 1000.000000000000227 ) ;
#11200=DIRECTION ( 'NONE',  ( -0.7071067811865487940, 0.7071067811865463515, -0.000000000000000000 ) ) ;
#11202=LINE ( 'NONE', #55484, #97264 ) ;
#11203=AXIS2_PLACEMENT_3D ( 'NONE', #25108, #125151, #112842 ) ;
#11204=CARTESIAN_POINT ( 'NONE',  ( -8.994519915287490619, 28.92564299267944250, 4.000000000000000000 ) ) ;
#11205=ORIENTED_EDGE ( 'NONE', *, *, #75456, .F. ) ;
#11206=VERTEX_POINT ( 'NONE', #23541 ) ;
#11208=FACE_OUTER_BOUND ( 'NONE', #888, .T. ) ;
#11211=AXIS2_PLACEMENT_3D ( 'NONE', #126441, #16226, #5366 ) ;
#11212=DIRECTION ( 'NONE',  ( -0.000000000000000000, 0.000000000000000000, 1.000000000000000000 ) ) ;
#11213=PLANE ( 'NONE',  #108163 ) ;
#11215=DIRECTION ( 'NONE',  ( 0.3543493200069162685, -0.000000000000000000, -0.9351131265310288487 ) ) ;
#11218=ORIENTED_EDGE ( 'NONE', *, *, #136515, .F. ) ;
#11220=CARTESIAN_POINT ( 'NONE',  ( 15.29974487139158867, -27.71228299555216879, 4.000000000000000000 ) ) ;
#11222=LINE ( 'NONE', #111268, #13831 ) ;
#11224=VECTOR ( 'NONE', #53101, 1000.000000000000000 ) ;
#11225=ORIENTED_EDGE ( 'NONE', *, *, #69089, .F. ) ;
#11226=EDGE_CURVE ( 'NONE', #77764, #60323, #12653, .T. ) ;
#11227=EDGE_CURVE ( 'NONE', #68726, #20176, #113388, .T. ) ;
#11229=ORIENTED_EDGE ( 'NONE', *, *, #92485, .F. ) ;
#11230=AXIS2_PLACEMENT_3D ( 'NONE', #3219, #90238, #134482 ) ;
#11231=FACE_OUTER_BOUND ( 'NONE', #77424, .T. ) ;
#11234=VECTOR ( 'NONE', #46421, 1000.000000000000000 ) ;
#11235=VERTEX_POINT ( 'NONE', #112690 ) ;
#11236=DIRECTION ( 'NONE',  ( -0.7071067811865487940, 0.7071067811865463515, 0.000000000000000000 ) ) ;
#11237=VECTOR ( 'NONE', #6356, 999.9999999999998863 ) ;
#11238=DIRECTION ( 'NONE',  ( -0.7071067811865486830, 0.7071067811865464625, 0.000000000000000000 ) ) ;
#11239=LINE ( 'NONE', #90254, #74392 ) ;
#11240=AXIS2_PLACEMENT_3D ( 'NONE', #36324, #31165, #63795 ) ;
#11241=EDGE_CURVE ( 'NONE', #71647, #24426, #47492, .T. ) ;
#11242=PLANE ( 'NONE',  #39431 ) ;
#11243=EDGE_CURVE ( 'NONE', #86591, #22993, #13356, .T. ) ;
#11244=CARTESIAN_POINT ( 'NONE',  ( -14.51078643762690490, -27.52281430457045275, 5.000000000000000000 ) ) ;
#11245=CARTESIAN_POINT ( 'NONE',  ( 8.510786437626906675, -27.52281430457049183, 5.000000000000000000 ) ) ;
#11246=EDGE_LOOP ( 'NONE', ( #94858, #78679, #40210, #8156 ) ) ;
#11248=DIRECTION ( 'NONE',  ( 0.7071067811865487940, 0.7071067811865463515, -0.000000000000000000 ) ) ;
#11250=CARTESIAN_POINT ( 'NONE',  ( 23.48860328114998453, 7.166961737892989959, 4.667035327419719160 ) ) ;
#11251=PLANE ( 'NONE',  #46143 ) ;
#11252=VECTOR ( 'NONE', #629, 1000.000000000000000 ) ;
#11253=ORIENTED_EDGE ( 'NONE', *, *, #116546, .F. ) ;
#11254=EDGE_CURVE ( 'NONE', #80031, #32625, #124284, .T. ) ;
#11255=ORIENTED_EDGE ( 'NONE', *, *, #42576, .F. ) ;
#11257=EDGE_LOOP ( 'NONE', ( #35928, #125200, #105636, #70712 ) ) ;
#11259=CARTESIAN_POINT ( 'NONE',  ( -5.292893218813420120, 5.259292476615661016, 5.000000000000000000 ) ) ;
#11263=EDGE_LOOP ( 'NONE', ( #100659, #86757, #106197, #120648 ) ) ;
#11264=ORIENTED_EDGE ( 'NONE', *, *, #110314, .F. ) ;
#11265=EDGE_CURVE ( 'NONE', #41140, #48586, #25675, .T. ) ;
#11266=VECTOR ( 'NONE', #133023, 1000.000000000000000 ) ;
#11267=DIRECTION ( 'NONE',  ( -0.6830127018922181881, 0.6830127018922202975, -0.2588190451025214056 ) ) ;
#11268=VERTEX_POINT ( 'NONE', #114120 ) ;
#11269=CARTESIAN_POINT ( 'NONE',  ( 69.18398860626899705, 28.73617430169835529, 5.000000000000000000 ) ) ;
#11272=DIRECTION ( 'NONE',  ( -0.000000000000000000, -0.3543493200069152693, 0.9351131265310292928 ) ) ;
#11273=ORIENTED_EDGE ( 'NONE', *, *, #12891, .T. ) ;
#11274=FACE_BOUND ( 'NONE', #139112, .T. ) ;
#11275=CARTESIAN_POINT ( 'NONE',  ( 14.81601139373099585, 28.73617430169776910, 5.000000000000000000 ) ) ;
#11276=EDGE_CURVE ( 'NONE', #120628, #116635, #85054, .T. ) ;
#11279=EDGE_CURVE ( 'NONE', #37795, #139420, #16953, .T. ) ;
#11280=DIRECTION ( 'NONE',  ( 0.3543493200069162685, -0.000000000000000000, -0.9351131265310288487 ) ) ;
#11281=FACE_OUTER_BOUND ( 'NONE', #141308, .T. ) ;
#11283=ADVANCED_FACE ( 'NONE', ( #82237 ), #50305, .F. ) ;
#11284=ORIENTED_EDGE ( 'NONE', *, *, #129750, .F. ) ;
#11285=ORIENTED_EDGE ( 'NONE', *, *, #61707, .T. ) ;
#11287=ORIENTED_EDGE ( 'NONE', *, *, #25478, .T. ) ;
#11288=VERTEX_POINT ( 'NONE', #137316 ) ;
#11289=DIRECTION ( 'NONE',  ( -0.000000000000000000, -0.3543493200069152693, 0.9351131265310292928 ) ) ;
#11290=CARTESIAN_POINT ( 'NONE',  ( 30.18398860626900060, 28.73617430169808173, 5.000000000000000000 ) ) ;
#11291=VERTEX_POINT ( 'NONE', #94492 ) ;
#11292=CARTESIAN_POINT ( 'NONE',  ( 34.45011844616453089, -17.99769585840587638, 5.000000000000001776 ) ) ;
#11293=DIRECTION ( 'NONE',  ( -0.6830127018922180770, -0.6830127018922204085, -0.2588190451025214056 ) ) ;
#11294=FACE_OUTER_BOUND ( 'NONE', #15248, .T. ) ;
#11295=DIRECTION ( 'NONE',  ( -0.000000000000000000, -0.3543493200069152693, 0.9351131265310292928 ) ) ;
#11296=DIRECTION ( 'NONE',  ( -0.7071067811865487940, 0.7071067811865463515, 0.000000000000000000 ) ) ;
#11298=VECTOR ( 'NONE', #30856, 1000.000000000000000 ) ;
#11299=CARTESIAN_POINT ( 'NONE',  ( -5.816011393731002066, 28.73617430169783304, 5.000000000000000000 ) ) ;
#11300=VECTOR ( 'NONE', #108244, 1000.000000000000000 ) ;
#11301=ORIENTED_EDGE ( 'NONE', *, *, #75926, .T. ) ;
#11302=DIRECTION ( 'NONE',  ( 0.7071067811865486830, -0.7071067811865464625, -0.000000000000000000 ) ) ;
#11303=CARTESIAN_POINT ( 'NONE',  ( -15.48921356237309510, -27.52281430457066236, 5.000000000000000000 ) ) ;
#11304=VECTOR ( 'NONE', #123147, 1000.000000000000000 ) ;
#11306=ORIENTED_EDGE ( 'NONE', *, *, #106985, .T. ) ;
#11307=ORIENTED_EDGE ( 'NONE', *, *, #18303, .T. ) ;
#11309=ORIENTED_EDGE ( 'NONE', *, *, #116652, .T. ) ;
#11314=DIRECTION ( 'NONE',  ( -0.3543493200069162685, -0.000000000000000000, -0.9351131265310288487 ) ) ;
#11315=ORIENTED_EDGE ( 'NONE', *, *, #39848, .T. ) ;
#11316=PLANE ( 'NONE',  #18655 ) ;
#11317=EDGE_CURVE ( 'NONE', #109641, #116177, #40845, .T. ) ;
#11318=VECTOR ( 'NONE', #52231, 1000.000000000000000 ) ;
#11319=VECTOR ( 'NONE', #85082, 999.9999999999998863 ) ;
#11320=DIRECTION ( 'NONE',  ( -0.6830127018922181881, 0.6830127018922202975, -0.2588190451025214056 ) ) ;
#11321=PLANE ( 'NONE',  #40568 ) ;
#11322=VERTEX_POINT ( 'NONE', #38707 ) ;
#11323=VECTOR ( 'NONE', #24116, 1000.000000000000227 ) ;
#11324=CARTESIAN_POINT ( 'NONE',  ( -8.999999999999941380, 7.931123077392104648, 4.000000000000000000 ) ) ;
#11325=FACE_OUTER_BOUND ( 'NONE', #6881, .T. ) ;
#11326=ORIENTED_EDGE ( 'NONE', *, *, #15356, .T. ) ;
#11328=VERTEX_POINT ( 'NONE', #82933 ) ;
#11330=VECTOR ( 'NONE', #127920, 1000.000000000000000 ) ;
#11331=VECTOR ( 'NONE', #141031, 1000.000000000000000 ) ;
#11332=DIRECTION ( 'NONE',  ( -0.000000000000000000, 0.000000000000000000, 1.000000000000000000 ) ) ;
#11334=EDGE_CURVE ( 'NONE', #14833, #58719, #62610, .T. ) ;
#11335=DIRECTION ( 'NONE',  ( 0.6830127018922180770, -0.6830127018922204085, -0.2588190451025213501 ) ) ;
#11336=ORIENTED_EDGE ( 'NONE', *, *, #123718, .T. ) ;
#11337=EDGE_CURVE ( 'NONE', #129172, #59038, #105371, .T. ) ;
#11338=CARTESIAN_POINT ( 'NONE',  ( 20.58838509405154582, 22.22500000000000853, 4.777194822843815913 ) ) ;
#11339=ORIENTED_EDGE ( 'NONE', *, *, #128639, .F. ) ;
#11340=VECTOR ( 'NONE', #98439, 1000.000000000000000 ) ;
#11344=EDGE_CURVE ( 'NONE', #110391, #63778, #51015, .T. ) ;
#11345=DIRECTION ( 'NONE',  ( -0.7071067811865486830, -0.7071067811865464625, -0.000000000000000000 ) ) ;
#11347=ORIENTED_EDGE ( 'NONE', *, *, #47910, .F. ) ;
#11349=CARTESIAN_POINT ( 'NONE',  ( -27.18398860626900060, 28.73617430169806042, 5.000000000000000000 ) ) ;
#11350=FACE_BOUND ( 'NONE', #38408, .T. ) ;
#11351=VECTOR ( 'NONE', #96578, 1000.000000000000227 ) ;
#11352=PLANE ( 'NONE',  #82075 ) ;
#11353=DIRECTION ( 'NONE',  ( -0.7071067811865486830, -0.7071067811865464625, 0.000000000000000000 ) ) ;
#11354=EDGE_CURVE ( 'NONE', #60934, #113076, #48880, .T. ) ;
#11355=PLANE ( 'NONE',  #43775 ) ;
#11356=CARTESIAN_POINT ( 'NONE',  ( 34.47516574401890921, 16.49051761211545752, 4.998110765256835286 ) ) ;
#11357=LINE ( 'NONE', #99836, #4638 ) ;
#11358=DIRECTION ( 'NONE',  ( -0.7071067811865487940, 0.7071067811865463515, 0.000000000000000000 ) ) ;
#11359=ORIENTED_EDGE ( 'NONE', *, *, #36713, .F. ) ;
#11360=CARTESIAN_POINT ( 'NONE',  ( -17.99999999999986855, -4.068876922607775448, 4.000000000000000000 ) ) ;
#11361=ORIENTED_EDGE ( 'NONE', *, *, #5244, .F. ) ;
#11362=ADVANCED_FACE ( 'NONE', ( #29242 ), #139486, .F. ) ;
#11363=EDGE_CURVE ( 'NONE', #87598, #36751, #72815, .T. ) ;
#11364=CARTESIAN_POINT ( 'NONE',  ( -2.816011393730999401, 28.73617430169785436, 5.000000000000000000 ) ) ;
#11365=ORIENTED_EDGE ( 'NONE', *, *, #59800, .F. ) ;
#11366=CARTESIAN_POINT ( 'NONE',  ( -33.48921356237309510, -27.52281430457078670, 5.000000000000000000 ) ) ;
#11367=CARTESIAN_POINT ( 'NONE',  ( -0.4892135623730947680, -27.52281430457055578, 5.000000000000000000 ) ) ;
#11368=ORIENTED_EDGE ( 'NONE', *, *, #131184, .F. ) ;
#11369=PLANE ( 'NONE',  #106477 ) ;
#11370=DIRECTION ( 'NONE',  ( 0.7071067811865487940, -0.7071067811865463515, 0.000000000000000000 ) ) ;
#11372=CARTESIAN_POINT ( 'NONE',  ( 34.92499999999998295, 9.759292476615621936, 4.255531930566176513 ) ) ;
#11374=CARTESIAN_POINT ( 'NONE',  ( 36.18398860626899705, 28.73617430169812437, 5.000000000000000000 ) ) ;
#11375=ORIENTED_EDGE ( 'NONE', *, *, #115461, .T. ) ;
#11376=CARTESIAN_POINT ( 'NONE',  ( -34.82816939922328459, -11.24070752338416135, 4.000000000000000000 ) ) ;
#11379=DIRECTION ( 'NONE',  ( -0.7071067811865486830, -0.7071067811865464625, 0.000000000000000000 ) ) ;
#11380=CARTESIAN_POINT ( 'NONE',  ( -2.843876922607561752, -22.22500000000000142, 4.000000000000000000 ) ) ;
#11381=CARTESIAN_POINT ( 'NONE',  ( 2.501836514860421801, -17.24070752338410273, 8.407044977365218941 ) ) ;
#11382=EDGE_CURVE ( 'NONE', #141849, #118741, #27102, .T. ) ;
#11383=CARTESIAN_POINT ( 'NONE',  ( 22.49999999999984723, -6.839392718269110105, -8.480912228396139341 ) ) ;
#11386=CARTESIAN_POINT ( 'NONE',  ( -24.49816348513941833, -17.24070752338410628, 8.407044977365281113 ) ) ;
#11387=DIRECTION ( 'NONE',  ( -0.000000000000000000, -0.3543493200069152693, 0.9351131265310292928 ) ) ;
#11388=ORIENTED_EDGE ( 'NONE', *, *, #120883, .T. ) ;
#11389=ADVANCED_FACE ( 'NONE', ( #18332 ), #15482, .F. ) ;
#11390=VERTEX_POINT ( 'NONE', #71345 ) ;
#11392=DIRECTION ( 'NONE',  ( -0.000000000000000000, -0.3543493200069152693, 0.9351131265310292928 ) ) ;
#11393=VERTEX_POINT ( 'NONE', #126411 ) ;
#11394=AXIS2_PLACEMENT_3D ( 'NONE', #18867, #107308, #23887 ) ;
#11396=CARTESIAN_POINT ( 'NONE',  ( -30.18398860626900060, 28.73617430169808173, 5.000000000000000000 ) ) ;
#11397=LINE ( 'NONE', #12845, #71818 ) ;
#11398=DIRECTION ( 'NONE',  ( -0.000000000000000000, 0.3543493200069153248, 0.9351131265310292928 ) ) ;
#11400=ORIENTED_EDGE ( 'NONE', *, *, #102313, .F. ) ;
#11401=VECTOR ( 'NONE', #77530, 1000.000000000000227 ) ;
#11403=EDGE_CURVE ( 'NONE', #106511, #50767, #116264, .T. ) ;
#11404=DIRECTION ( 'NONE',  ( -0.3543493200069162685, -0.000000000000000000, -0.9351131265310288487 ) ) ;
#11405=AXIS2_PLACEMENT_3D ( 'NONE', #121512, #21510, #99768 ) ;
#11406=CARTESIAN_POINT ( 'NONE',  ( -22.17183060077631751, -14.24070752338413293, 4.000000000000000000 ) ) ;
#11407=EDGE_CURVE ( 'NONE', #21343, #16391, #5335, .T. ) ;
#11408=PLANE ( 'NONE',  #20768 ) ;
#11409=EDGE_CURVE ( 'NONE', #17718, #122293, #26935, .T. ) ;
#11411=PLANE ( 'NONE',  #89163 ) ;
#11412=ORIENTED_EDGE ( 'NONE', *, *, #20737, .F. ) ;
#11413=CARTESIAN_POINT ( 'NONE',  ( 15.18398860626900237, 28.73617430169797871, 5.000000000000000000 ) ) ;
#11414=CARTESIAN_POINT ( 'NONE',  ( 19.60343192894631414, -14.24070752338413293, 19.24067776001730223 ) ) ;
#11415=LINE ( 'NONE', #53541, #93260 ) ;
#11416=FACE_OUTER_BOUND ( 'NONE', #22922, .T. ) ;
#11417=VECTOR ( 'NONE', #123237, 1000.000000000000000 ) ;
#11418=PLANE ( 'NONE',  #9900 ) ;
#11419=ORIENTED_EDGE ( 'NONE', *, *, #2742, .F. ) ;
#11420=VERTEX_POINT ( 'NONE', #17636 ) ;
#11423=EDGE_CURVE ( 'NONE', #56879, #16801, #97325, .T. ) ;
#11424=ORIENTED_EDGE ( 'NONE', *, *, #66726, .F. ) ;
#11426=LINE ( 'NONE', #45563, #125002 ) ;
#11427=DIRECTION ( 'NONE',  ( 0.3543493200069162685, -0.000000000000000000, -0.9351131265310288487 ) ) ;
#11428=VECTOR ( 'NONE', #52071, 1000.000000000000114 ) ;
#11429=VECTOR ( 'NONE', #26378, 1000.000000000000227 ) ;
#11430=FACE_OUTER_BOUND ( 'NONE', #82029, .T. ) ;
#11431=FACE_OUTER_BOUND ( 'NONE', #5771, .T. ) ;
#11432=VERTEX_POINT ( 'NONE', #29946 ) ;
#11433=EDGE_CURVE ( 'NONE', #98689, #2221, #138190, .T. ) ;
#11434=DIRECTION ( 'NONE',  ( -0.000000000000000000, 0.3543493200069153248, 0.9351131265310292928 ) ) ;
#11435=LINE ( 'NONE', #75321, #136851 ) ;
#11436=( BOUNDED_CURVE ( )  B_SPLINE_CURVE ( 3, ( #52247, #63163, #129804, #19616 ),
 .UNSPECIFIED., .F., .F. ) 
 B_SPLINE_CURVE_WITH_KNOTS ( ( 4, 4 ),
 ( 5.043186909253406291, 5.074607125596347856 ),
 .UNSPECIFIED. ) 
 CURVE ( )  GEOMETRIC_REPRESENTATION_ITEM ( )  RATIONAL_B_SPLINE_CURVE ( ( 1.000000000000000000, 0.9999177325257868620, 0.9999177325257868620, 1.000000000000000000 ) ) 
 REPRESENTATION_ITEM ( '' )  );
#11437=VECTOR ( 'NONE', #130944, 1000.000000000000227 ) ;
#11439=EDGE_LOOP ( 'NONE', ( #65281, #74381, #72542, #22901 ) ) ;
#11440=DIRECTION ( 'NONE',  ( 0.7071067811865487940, -0.7071067811865463515, 0.000000000000000000 ) ) ;
#11441=CARTESIAN_POINT ( 'NONE',  ( -33.31657961132769685, -6.740707523384209310, 11.88629033278132496 ) ) ;
#11442=AXIS2_PLACEMENT_3D ( 'NONE', #8064, #96487, #108795 ) ;
#11443=AXIS2_PLACEMENT_3D ( 'NONE', #87914, #11757, #19794 ) ;
#11445=VERTEX_POINT ( 'NONE', #8857 ) ;
#11446=ORIENTED_EDGE ( 'NONE', *, *, #92415, .F. ) ;
#11447=ORIENTED_EDGE ( 'NONE', *, *, #128759, .T. ) ;
#11448=CARTESIAN_POINT ( 'NONE',  ( -57.48921356237308800, -27.52281430457095368, 5.000000000000000000 ) ) ;
#11449=VECTOR ( 'NONE', #127138, 1000.000000000000227 ) ;
#11450=DIRECTION ( 'NONE',  ( -0.3543493200069163795, -9.265275131829747941E-33, -0.9351131265310288487 ) ) ;
#11454=CARTESIAN_POINT ( 'NONE',  ( -10.49999999999992539, 13.46639925780212366, 5.000000000000000000 ) ) ;
#11456=EDGE_CURVE ( 'NONE', #99319, #127035, #119796, .T. ) ;
#11458=EDGE_CURVE ( 'NONE', #46893, #59884, #131429, .T. ) ;
#11459=VERTEX_POINT ( 'NONE', #120498 ) ;
#11460=EDGE_LOOP ( 'NONE', ( #66438, #10459, #115132, #124448 ) ) ;
#11462=VERTEX_POINT ( 'NONE', #75623 ) ;
#11463=ORIENTED_EDGE ( 'NONE', *, *, #111778, .F. ) ;
#11464=AXIS2_PLACEMENT_3D ( 'NONE', #138369, #108371, #1746 ) ;
#11465=EDGE_CURVE ( 'NONE', #58699, #71262, #43697, .T. ) ;
#11466=DIRECTION ( 'NONE',  ( -0.7071067811865486830, -0.7071067811865464625, 0.000000000000000000 ) ) ;
#11468=FACE_OUTER_BOUND ( 'NONE', #31486, .T. ) ;
#11469=LINE ( 'NONE', #78206, #3125 ) ;
#11470=CARTESIAN_POINT ( 'NONE',  ( 34.42499999999998295, -19.45860074219776692, 5.000000000000000000 ) ) ;
#11473=ORIENTED_EDGE ( 'NONE', *, *, #53467, .T. ) ;
#11474=FACE_OUTER_BOUND ( 'NONE', #49991, .T. ) ;
#11475=ORIENTED_EDGE ( 'NONE', *, *, #137002, .F. ) ;
#11476=FACE_OUTER_BOUND ( 'NONE', #73966, .T. ) ;
#11479=VERTEX_POINT ( 'NONE', #107518 ) ;
#11480=DIRECTION ( 'NONE',  ( 0.3543493200069162685, -0.000000000000000000, -0.9351131265310288487 ) ) ;
#11481=ORIENTED_EDGE ( 'NONE', *, *, #29731, .T. ) ;
#11482=ORIENTED_EDGE ( 'NONE', *, *, #116056, .F. ) ;
#11483=ORIENTED_EDGE ( 'NONE', *, *, #19732, .F. ) ;
#11484=DIRECTION ( 'NONE',  ( 0.6830127018922181881, 0.6830127018922202975, -0.2588190451025214056 ) ) ;
#11485=DIRECTION ( 'NONE',  ( -0.7071067811865486830, -0.7071067811865464625, -0.000000000000000000 ) ) ;
#11487=FACE_OUTER_BOUND ( 'NONE', #14834, .T. ) ;
#11488=DIRECTION ( 'NONE',  ( 0.7071067811865487940, 0.7071067811865463515, 0.000000000000000000 ) ) ;
#11489=CARTESIAN_POINT ( 'NONE',  ( 24.18398860626899705, 28.73617430169804265, 5.000000000000000000 ) ) ;
#11490=DIRECTION ( 'NONE',  ( 0.7071067811865486830, -0.7071067811865464625, -0.000000000000000000 ) ) ;
#11491=CARTESIAN_POINT ( 'NONE',  ( -29.99999999999979039, 1.761378380278656675, -6.096875308897323542 ) ) ;
#11492=EDGE_LOOP ( 'NONE', ( #101238, #139912, #32168, #122033 ) ) ;
#11493=DIRECTION ( 'NONE',  ( -0.7071067811865486830, -0.7071067811865464625, 0.000000000000000000 ) ) ;
#11494=PLANE ( 'NONE',  #7772 ) ;
#11495=ORIENTED_EDGE ( 'NONE', *, *, #4997, .T. ) ;
#11496=ORIENTED_EDGE ( 'NONE', *, *, #32543, .F. ) ;
#11497=VERTEX_POINT ( 'NONE', #98084 ) ;
#11498=LINE ( 'NONE', #111566, #91202 ) ;
#11499=AXIS2_PLACEMENT_3D ( 'NONE', #119047, #129202, #95152 ) ;
#11500=VECTOR ( 'NONE', #99078, 1000.000000000000000 ) ;
#11501=ORIENTED_EDGE ( 'NONE', *, *, #129106, .F. ) ;
#11502=VECTOR ( 'NONE', #106469, 1000.000000000000227 ) ;
#11503=AXIS2_PLACEMENT_3D ( 'NONE', #17570, #71279, #129188 ) ;
#11504=EDGE_CURVE ( 'NONE', #92319, #65131, #132155, .T. ) ;
#11505=ORIENTED_EDGE ( 'NONE', *, *, #112209, .T. ) ;
#11506=LINE ( 'NONE', #134054, #58402 ) ;
#11507=PLANE ( 'NONE',  #75677 ) ;
#11508=FACE_OUTER_BOUND ( 'NONE', #21459, .T. ) ;
#11509=ADVANCED_FACE ( 'NONE', ( #98770 ), #21227, .F. ) ;
#11510=LINE ( 'NONE', #55792, #75082 ) ;
#11511=LINE ( 'NONE', #55793, #92651 ) ;
#11512=ORIENTED_EDGE ( 'NONE', *, *, #48108, .F. ) ;
#11513=CARTESIAN_POINT ( 'NONE',  ( -13.82816939922343025, -8.240707523384196875, 4.000000000000000000 ) ) ;
#11514=AXIS2_PLACEMENT_3D ( 'NONE', #55496, #112016, #111263 ) ;
#11515=ORIENTED_EDGE ( 'NONE', *, *, #20664, .T. ) ;
#11516=DIRECTION ( 'NONE',  ( -1.000000000000000000, 0.000000000000000000, -0.000000000000000000 ) ) ;
#11517=EDGE_CURVE ( 'NONE', #112409, #41303, #141592, .T. ) ;
#11518=EDGE_CURVE ( 'NONE', #94849, #138021, #44447, .T. ) ;
#11520=ORIENTED_EDGE ( 'NONE', *, *, #68335, .T. ) ;
#11522=DIRECTION ( 'NONE',  ( -0.6830127018922181881, 0.6830127018922202975, -0.2588190451025214056 ) ) ;
#11523=EDGE_CURVE ( 'NONE', #95983, #14590, #32848, .T. ) ;
#11524=DIRECTION ( 'NONE',  ( -0.000000000000000000, -0.3543493200069152693, 0.9351131265310292928 ) ) ;
#11525=VERTEX_POINT ( 'NONE', #109663 ) ;
#11526=ORIENTED_EDGE ( 'NONE', *, *, #95553, .T. ) ;
#11528=DIRECTION ( 'NONE',  ( -0.7071067811865486830, 0.7071067811865464625, 0.000000000000000000 ) ) ;
#11530=PLANE ( 'NONE',  #125061 ) ;
#11531=AXIS2_PLACEMENT_3D ( 'NONE', #106687, #84288, #128483 ) ;
#11532=PLANE ( 'NONE',  #76638 ) ;
#11534=CARTESIAN_POINT ( 'NONE',  ( -1.499999999999990896, 3.431123077392149501, 4.000000000000000000 ) ) ;
#11535=VERTEX_POINT ( 'NONE', #77071 ) ;
#11536=CARTESIAN_POINT ( 'NONE',  ( 36.48921356237310221, -27.52281430457080802, 5.000000000000000000 ) ) ;
#11537=EDGE_CURVE ( 'NONE', #88432, #12339, #110352, .T. ) ;
#11538=PLANE ( 'NONE',  #67455 ) ;
#11539=DIRECTION ( 'NONE',  ( -0.7071067811865486830, -0.7071067811865464625, -0.000000000000000000 ) ) ;
#11540=ORIENTED_EDGE ( 'NONE', *, *, #52236, .T. ) ;
#11541=CARTESIAN_POINT ( 'NONE',  ( -12.29974487139158512, -27.71228299555214747, 4.000000000000000000 ) ) ;
#11542=ADVANCED_FACE ( 'NONE', ( #130733 ), #31400, .T. ) ;
#11543=CARTESIAN_POINT ( 'NONE',  ( -34.92500000000001137, -22.22500000000000142, 4.000000000000000000 ) ) ;
#11544=VECTOR ( 'NONE', #68884, 1000.000000000000000 ) ;
#11545=ORIENTED_EDGE ( 'NONE', *, *, #8084, .T. ) ;
#11546=PLANE ( 'NONE',  #69518 ) ;
#11548=VERTEX_POINT ( 'NONE', #11027 ) ;
#11549=CARTESIAN_POINT ( 'NONE',  ( 31.98012225071433789, -17.24070752338409562, 20.23474786156476313 ) ) ;
#11551=CARTESIAN_POINT ( 'NONE',  ( 26.99999999999981526, -18.41253812416056590, 4.000000000000000000 ) ) ;
#11552=EDGE_CURVE ( 'NONE', #949, #112797, #52417, .T. ) ;
#11553=ORIENTED_EDGE ( 'NONE', *, *, #30145, .T. ) ;
#11555=LINE ( 'NONE', #100042, #15052 ) ;
#11556=CARTESIAN_POINT ( 'NONE',  ( -25.49999999999982592, -12.66682484999669178, -0.6294897503864504973 ) ) ;
#11557=VECTOR ( 'NONE', #20580, 1000.000000000000000 ) ;
#11558=FACE_OUTER_BOUND ( 'NONE', #91823, .T. ) ;
#11559=FACE_OUTER_BOUND ( 'NONE', #51733, .T. ) ;
#11560=DIRECTION ( 'NONE',  ( 0.6830127018922181881, 0.6830127018922202975, -0.2588190451025214056 ) ) ;
#11561=FACE_OUTER_BOUND ( 'NONE', #133698, .T. ) ;
#11562=EDGE_CURVE ( 'NONE', #11751, #35892, #143008, .T. ) ;
#11563=CARTESIAN_POINT ( 'NONE',  ( 19.49999999999987210, -11.94781430457070215, 5.000000000000000000 ) ) ;
#11565=VECTOR ( 'NONE', #24100, 1000.000000000000000 ) ;
#11566=LINE ( 'NONE', #53701, #127750 ) ;
#11567=DIRECTION ( 'NONE',  ( -0.000000000000000000, 0.000000000000000000, 1.000000000000000000 ) ) ;
#11568=CARTESIAN_POINT ( 'NONE',  ( -2.292986735706930457, -21.74070752338405299, 4.999753212805217117 ) ) ;
#11569=LINE ( 'NONE', #55850, #29171 ) ;
#11570=ORIENTED_EDGE ( 'NONE', *, *, #119608, .T. ) ;
#11571=EDGE_LOOP ( 'NONE', ( #91312, #74018, #129542, #51838 ) ) ;
#11572=EDGE_CURVE ( 'NONE', #138595, #68933, #30703, .T. ) ;
#11574=VERTEX_POINT ( 'NONE', #87203 ) ;
#11576=EDGE_CURVE ( 'NONE', #51437, #139749, #64029, .T. ) ;
#11577=ORIENTED_EDGE ( 'NONE', *, *, #3520, .F. ) ;
#11578=DIRECTION ( 'NONE',  ( -0.000000000000000000, 0.3543493200069153248, 0.9351131265310292928 ) ) ;
#11579=PLANE ( 'NONE',  #143499 ) ;
#11580=AXIS2_PLACEMENT_3D ( 'NONE', #77709, #110294, #98717 ) ;
#11581=ORIENTED_EDGE ( 'NONE', *, *, #126480, .T. ) ;
#11583=EDGE_CURVE ( 'NONE', #10965, #11574, #77767, .T. ) ;
#11585=CARTESIAN_POINT ( 'NONE',  ( 0.000000000000000000, 0.000000000000000000, 5.000000000000000000 ) ) ;
#11586=DIRECTION ( 'NONE',  ( -0.7071067811865486830, -0.7071067811865464625, 0.000000000000000000 ) ) ;
#11588=CARTESIAN_POINT ( 'NONE',  ( 1.499999999999992673, -1.912538124160737318, 4.000000000000000000 ) ) ;
#11589=FACE_OUTER_BOUND ( 'NONE', #38532, .T. ) ;
#11590=LINE ( 'NONE', #727, #15069 ) ;
#11592=DIRECTION ( 'NONE',  ( -0.000000000000000000, 0.000000000000000000, 1.000000000000000000 ) ) ;
#11595=DIRECTION ( 'NONE',  ( -0.3543493200069162685, -0.000000000000000000, -0.9351131265310288487 ) ) ;
#11596=ORIENTED_EDGE ( 'NONE', *, *, #47022, .F. ) ;
#11597=ORIENTED_EDGE ( 'NONE', *, *, #137614, .T. ) ;
#11599=VERTEX_POINT ( 'NONE', #22617 ) ;
#11600=EDGE_CURVE ( 'NONE', #34867, #5353, #67628, .T. ) ;
#11601=FACE_OUTER_BOUND ( 'NONE', #45914, .T. ) ;
#11603=ADVANCED_FACE ( 'NONE', ( #112521 ), #133574, .F. ) ;
#11605=AXIS2_PLACEMENT_3D ( 'NONE', #20813, #132489, #121552 ) ;
#11607=EDGE_LOOP ( 'NONE', ( #45508, #79874, #94444, #78458 ) ) ;
#11608=AXIS2_PLACEMENT_3D ( 'NONE', #58249, #124878, #101690 ) ;
#11609=ORIENTED_EDGE ( 'NONE', *, *, #32765, .F. ) ;
#11610=LINE ( 'NONE', #34131, #131847 ) ;
#11611=VECTOR ( 'NONE', #55070, 1000.000000000000000 ) ;
#11612=VECTOR ( 'NONE', #43499, 999.9999999999998863 ) ;
#11614=DIRECTION ( 'NONE',  ( -0.7071067811865486830, -0.7071067811865464625, 0.000000000000000000 ) ) ;
#11615=VECTOR ( 'NONE', #36843, 1000.000000000000227 ) ;
#11617=ORIENTED_EDGE ( 'NONE', *, *, #40425, .T. ) ;
#11619=ORIENTED_EDGE ( 'NONE', *, *, #119887, .F. ) ;
#11620=FACE_OUTER_BOUND ( 'NONE', #6820, .T. ) ;
#11621=CARTESIAN_POINT ( 'NONE',  ( -34.45011844616455221, -8.997695858405947433, 5.000000000000000888 ) ) ;
#11622=LINE ( 'NONE', #120376, #36882 ) ;
#11623=VECTOR ( 'NONE', #84220, 999.9999999999998863 ) ;
#11625=EDGE_CURVE ( 'NONE', #67882, #25495, #24094, .T. ) ;
#11627=EDGE_LOOP ( 'NONE', ( #4065, #121174, #94175, #121391 ) ) ;
#11628=CARTESIAN_POINT ( 'NONE',  ( -24.18398860626899705, 28.73617430169804265, 5.000000000000000000 ) ) ;
#11629=EDGE_LOOP ( 'NONE', ( #119563, #90667, #121590, #1960 ) ) ;
#11630=ORIENTED_EDGE ( 'NONE', *, *, #140323, .F. ) ;
#11631=VECTOR ( 'NONE', #115887, 1000.000000000000227 ) ;
#11632=ORIENTED_EDGE ( 'NONE', *, *, #90330, .T. ) ;
#11633=AXIS2_PLACEMENT_3D ( 'NONE', #17675, #95255, #37326 ) ;
#11634=VECTOR ( 'NONE', #134203, 1000.000000000000000 ) ;
#11635=CARTESIAN_POINT ( 'NONE',  ( -29.99999999999979039, -18.41253812416056235, 4.000000000000000000 ) ) ;
#11636=CARTESIAN_POINT ( 'NONE',  ( 29.29289321881325137, 11.25929247661560773, 5.000000000000000000 ) ) ;
#11638=PLANE ( 'NONE',  #71476 ) ;
#11639=AXIS2_PLACEMENT_3D ( 'NONE', #136583, #46049, #101828 ) ;
#11640=CARTESIAN_POINT ( 'NONE',  ( 32.20710678118632586, 12.75929247661558641, 5.000000000000000000 ) ) ;
#11641=CARTESIAN_POINT ( 'NONE',  ( -5.999999999999970690, 20.58746187583905041, 4.000000000000000000 ) ) ;
#11642=VECTOR ( 'NONE', #98254, 1000.000000000000000 ) ;
#11643=LINE ( 'NONE', #87806, #18904 ) ;
#11644=FACE_BOUND ( 'NONE', #78172, .T. ) ;
#11645=ORIENTED_EDGE ( 'NONE', *, *, #2203, .T. ) ;
#11648=CARTESIAN_POINT ( 'NONE',  ( 34.49999999999975131, -16.91253812416058366, 4.000000000000000000 ) ) ;
#11649=CARTESIAN_POINT ( 'NONE',  ( 48.48921356237309510, -27.52281430457089328, 5.000000000000000000 ) ) ;
#11650=ORIENTED_EDGE ( 'NONE', *, *, #42681, .T. ) ;
#11651=PLANE ( 'NONE',  #48110 ) ;
#11652=EDGE_LOOP ( 'NONE', ( #140346, #104251, #70753, #43258 ) ) ;
#11653=ORIENTED_EDGE ( 'NONE', *, *, #88314, .T. ) ;
#11654=ORIENTED_EDGE ( 'NONE', *, *, #26515, .F. ) ;
#11656=ORIENTED_EDGE ( 'NONE', *, *, #118139, .T. ) ;
#11657=VECTOR ( 'NONE', #137312, 1000.000000000000114 ) ;
#11659=CARTESIAN_POINT ( 'NONE',  ( 42.29974487139158157, -27.71228299555235708, 4.000000000000000000 ) ) ;
#11660=DIRECTION ( 'NONE',  ( -0.7071067811865486830, 0.7071067811865464625, 0.000000000000000000 ) ) ;
#11661=ORIENTED_EDGE ( 'NONE', *, *, #14904, .F. ) ;
#11663=VECTOR ( 'NONE', #45710, 1000.000000000000227 ) ;
#11664=FACE_OUTER_BOUND ( 'NONE', #125779, .T. ) ;
#11665=CARTESIAN_POINT ( 'NONE',  ( 30.18398860626900060, 28.73617430169808173, 5.000000000000000000 ) ) ;
#11666=DIRECTION ( 'NONE',  ( 0.3543493200069162685, -0.000000000000000000, -0.9351131265310288487 ) ) ;
#11668=CARTESIAN_POINT ( 'NONE',  ( 19.49999999999987210, -8.947814304570730570, 5.000000000000000000 ) ) ;
#11670=VERTEX_POINT ( 'NONE', #34989 ) ;
#11671=EDGE_CURVE ( 'NONE', #53073, #90399, #90794, .T. ) ;
#11672=ORIENTED_EDGE ( 'NONE', *, *, #40867, .F. ) ;
#11673=AXIS2_PLACEMENT_3D ( 'NONE', #15956, #71123, #137802 ) ;
#11674=VERTEX_POINT ( 'NONE', #78477 ) ;
#11675=CARTESIAN_POINT ( 'NONE',  ( 9.489213562373095101, -27.52281430457062328, 5.000000000000000000 ) ) ;
#11676=CARTESIAN_POINT ( 'NONE',  ( -38.95341186370431785, 14.25929247661557042, 18.84478104361336648 ) ) ;
#11678=ORIENTED_EDGE ( 'NONE', *, *, #70497, .F. ) ;
#11679=FACE_OUTER_BOUND ( 'NONE', #36786, .T. ) ;
#11681=ADVANCED_FACE ( 'NONE', ( #103082 ), #25496, .F. ) ;
#11682=EDGE_CURVE ( 'NONE', #86567, #3709, #68350, .T. ) ;
#11683=DIRECTION ( 'NONE',  ( 0.7071067811865487940, 0.7071067811865463515, 0.000000000000000000 ) ) ;
#11684=ORIENTED_EDGE ( 'NONE', *, *, #19721, .T. ) ;
#11685=LINE ( 'NONE', #99418, #4606 ) ;
#11686=VECTOR ( 'NONE', #31194, 1000.000000000000114 ) ;
#11688=EDGE_CURVE ( 'NONE', #48357, #73550, #132880, .T. ) ;
#11692=ADVANCED_FACE ( 'NONE', ( #80626 ), #124826, .F. ) ;
#11693=ORIENTED_EDGE ( 'NONE', *, *, #84416, .T. ) ;
#11695=EDGE_CURVE ( 'NONE', #37816, #29497, #95032, .T. ) ;
#11696=LINE ( 'NONE', #66836, #44275 ) ;
#11697=CARTESIAN_POINT ( 'NONE',  ( 4.371765549556129393, -8.240707523384200428, 11.38925528200751458 ) ) ;
#11698=PLANE ( 'NONE',  #67793 ) ;
#11699=VERTEX_POINT ( 'NONE', #5151 ) ;
#11700=DIRECTION ( 'NONE',  ( 0.7071067811865487940, 0.7071067811865463515, 0.000000000000000000 ) ) ;
#11701=ORIENTED_EDGE ( 'NONE', *, *, #134051, .F. ) ;
#11703=DIRECTION ( 'NONE',  ( 0.7071067811865487940, 0.7071067811865463515, 0.000000000000000000 ) ) ;
#11704=CARTESIAN_POINT ( 'NONE',  ( -34.92500000000001137, -8.143876922607470092, 4.000000000000000000 ) ) ;
#11705=DIRECTION ( 'NONE',  ( -0.7071067811865486830, -0.7071067811865464625, -0.000000000000000000 ) ) ;
#11708=DIRECTION ( 'NONE',  ( 0.7071067811865486830, -0.7071067811865464625, -0.000000000000000000 ) ) ;
#11709=EDGE_CURVE ( 'NONE', #14462, #143141, #71907, .T. ) ;
#11711=DIRECTION ( 'NONE',  ( -1.000000000000000000, -4.708078457166071843E-14, 0.000000000000000000 ) ) ;
#11712=PLANE ( 'NONE',  #90793 ) ;
#11714=AXIS2_PLACEMENT_3D ( 'NONE', #56000, #89311, #66850 ) ;
#11717=VECTOR ( 'NONE', #10895, 1000.000000000000227 ) ;
#11719=VECTOR ( 'NONE', #13466, 1000.000000000000227 ) ;
#11720=ORIENTED_EDGE ( 'NONE', *, *, #68771, .F. ) ;
#11721=ADVANCED_FACE ( 'NONE', ( #116080 ), #15316, .F. ) ;
#11723=DIRECTION ( 'NONE',  ( 0.3543493200069163240, 0.000000000000000000, 0.9351131265310288487 ) ) ;
#11725=ORIENTED_EDGE ( 'NONE', *, *, #56208, .F. ) ;
#11726=CARTESIAN_POINT ( 'NONE',  ( -30.29974487139158867, -27.71228299555227537, 4.000000000000000000 ) ) ;
#11727=VECTOR ( 'NONE', #98299, 1000.000000000000000 ) ;
#11728=LINE ( 'NONE', #3014, #126936 ) ;
#11729=EDGE_CURVE ( 'NONE', #64057, #106060, #70503, .T. ) ;
#11731=LINE ( 'NONE', #56015, #48323 ) ;
#11732=CARTESIAN_POINT ( 'NONE',  ( -28.49999999999979750, 10.94296225409023826, -9.576120664313320319 ) ) ;
#11733=CARTESIAN_POINT ( 'NONE',  ( 18.48921356237309510, -27.52281430457068367, 5.000000000000000000 ) ) ;
#11734=ORIENTED_EDGE ( 'NONE', *, *, #61538, .F. ) ;
#11736=DIRECTION ( 'NONE',  ( -0.6830127018922180770, -0.6830127018922204085, -0.2588190451025213501 ) ) ;
#11737=LINE ( 'NONE', #55289, #67615 ) ;
#11738=CARTESIAN_POINT ( 'NONE',  ( -2.999999999999975131, 15.45873954670185135, -0.03131636524293310297 ) ) ;
#11740=LINE ( 'NONE', #109652, #80760 ) ;
#11742=CARTESIAN_POINT ( 'NONE',  ( 4.998069433178977228, -22.22500000000000142, 4.500000000000000888 ) ) ;
#11743=AXIS2_PLACEMENT_3D ( 'NONE', #122372, #25943, #103471 ) ;
#11746=ADVANCED_FACE ( 'NONE', ( #126260 ), #39263, .F. ) ;
#11747=AXIS2_PLACEMENT_3D ( 'NONE', #143050, #141639, #96647 ) ;
#11748=ORIENTED_EDGE ( 'NONE', *, *, #88926, .T. ) ;
#11749=EDGE_CURVE ( 'NONE', #137381, #76116, #137141, .T. ) ;
#11750=VECTOR ( 'NONE', #123448, 1000.000000000000000 ) ;
#11751=VERTEX_POINT ( 'NONE', #115331 ) ;
#11752=DIRECTION ( 'NONE',  ( 0.7071067811865487940, 0.7071067811865463515, -0.000000000000000000 ) ) ;
#11753=LINE ( 'NONE', #12483, #78735 ) ;
#11754=VECTOR ( 'NONE', #20314, 1000.000000000000000 ) ;
#11755=ORIENTED_EDGE ( 'NONE', *, *, #133037, .T. ) ;
#11756=EDGE_CURVE ( 'NONE', #74522, #42386, #137866, .T. ) ;
#11757=DIRECTION ( 'NONE',  ( -0.000000000000000000, 0.000000000000000000, 1.000000000000000000 ) ) ;
#11758=PLANE ( 'NONE',  #14222 ) ;
#11759=EDGE_CURVE ( 'NONE', #135854, #84525, #84214, .T. ) ;
#11760=FACE_OUTER_BOUND ( 'NONE', #101406, .T. ) ;
#11761=DIRECTION ( 'NONE',  ( -0.7071067811865486830, -0.7071067811865464625, 0.000000000000000000 ) ) ;
#11763=VECTOR ( 'NONE', #14064, 1000.000000000000000 ) ;
#11764=EDGE_LOOP ( 'NONE', ( #43205, #138969, #133033, #24722 ) ) ;
#11767=DIRECTION ( 'NONE',  ( 0.7071067811865487940, 0.7071067811865463515, 0.000000000000000000 ) ) ;
#11769=CARTESIAN_POINT ( 'NONE',  ( 7.499999999999960032, 1.087461875839230707, 4.000000000000000000 ) ) ;
#11770=DIRECTION ( 'NONE',  ( -0.7071067811865486830, -0.7071067811865464625, 0.000000000000000000 ) ) ;
#11771=CARTESIAN_POINT ( 'NONE',  ( -34.92500000000001137, -22.22500000000000142, 4.000000000000000000 ) ) ;
#11773=CARTESIAN_POINT ( 'NONE',  ( -34.92500000000001137, 16.51246187583933533, 4.000000000000000000 ) ) ;
#11774=PLANE ( 'NONE',  #55468 ) ;
#11775=AXIS2_PLACEMENT_3D ( 'NONE', #85051, #19081, #130730 ) ;
#11776=VERTEX_POINT ( 'NONE', #73322 ) ;
#11779=EDGE_CURVE ( 'NONE', #142313, #3243, #61056, .T. ) ;
#11780=DIRECTION ( 'NONE',  ( 1.000000000000000000, 0.000000000000000000, 0.000000000000000000 ) ) ;
#11782=CARTESIAN_POINT ( 'NONE',  ( -30.18398860626900060, 28.73617430169808173, 5.000000000000000000 ) ) ;
#11784=VECTOR ( 'NONE', #47292, 1000.000000000000000 ) ;
#11786=DIRECTION ( 'NONE',  ( 0.7071067811865486830, -0.7071067811865464625, -0.000000000000000000 ) ) ;
#11788=EDGE_CURVE ( 'NONE', #100098, #116562, #9430, .T. ) ;
#11789=EDGE_LOOP ( 'NONE', ( #41158, #73228, #56972, #89183 ) ) ;
#11791=VERTEX_POINT ( 'NONE', #31942 ) ;
#11792=ORIENTED_EDGE ( 'NONE', *, *, #79705, .T. ) ;
#11793=PLANE ( 'NONE',  #56223 ) ;
#11794=CARTESIAN_POINT ( 'NONE',  ( -34.92500000000001137, -22.22500000000000142, 4.000000000000000000 ) ) ;
#11795=CARTESIAN_POINT ( 'NONE',  ( 19.05000000000000071, 3.174999999999997158, 4.000000000000000000 ) ) ;
#11796=DIRECTION ( 'NONE',  ( -0.7071067811865486830, -0.7071067811865463515, 0.000000000000000000 ) ) ;
#11797=EDGE_LOOP ( 'NONE', ( #127209, #90395, #56898, #39550 ) ) ;
#11798=ADVANCED_FACE ( 'NONE', ( #64567 ), #7304, .F. ) ;
#11799=DIRECTION ( 'NONE',  ( -0.3543493200069163240, -0.000000000000000000, 0.9351131265310288487 ) ) ;
#11802=DIRECTION ( 'NONE',  ( -0.7071067811865487940, 0.7071067811865463515, -0.000000000000000000 ) ) ;
#11803=DIRECTION ( 'NONE',  ( 0.6830127018922181881, 0.6830127018922202975, -0.2588190451025214056 ) ) ;
#11804=DIRECTION ( 'NONE',  ( 1.000000000000000000, 0.000000000000000000, 0.000000000000000000 ) ) ;
#11805=LINE ( 'NONE', #121999, #76445 ) ;
#11806=VECTOR ( 'NONE', #129108, 1000.000000000000227 ) ;
#11807=VERTEX_POINT ( 'NONE', #63179 ) ;
#11808=CARTESIAN_POINT ( 'NONE',  ( -51.48921356237309510, -27.52281430457091460, 5.000000000000000000 ) ) ;
#11810=LINE ( 'NONE', #24147, #53337 ) ;
#11811=CARTESIAN_POINT ( 'NONE',  ( 0.000000000000000000, 0.000000000000000000, 5.000000000000000000 ) ) ;
#11812=FACE_OUTER_BOUND ( 'NONE', #135836, .T. ) ;
#11813=ORIENTED_EDGE ( 'NONE', *, *, #112682, .T. ) ;
#11814=FACE_OUTER_BOUND ( 'NONE', #52365, .T. ) ;
#11815=VECTOR ( 'NONE', #64515, 1000.000000000000000 ) ;
#11816=ORIENTED_EDGE ( 'NONE', *, *, #43594, .T. ) ;
#11818=AXIS2_PLACEMENT_3D ( 'NONE', #25056, #35977, #124389 ) ;
#11819=VECTOR ( 'NONE', #115041, 1000.000000000000000 ) ;
#11820=EDGE_CURVE ( 'NONE', #40982, #28348, #52951, .T. ) ;
#11822=EDGE_LOOP ( 'NONE', ( #61125, #2281, #119925, #96590 ) ) ;
#11823=LINE ( 'NONE', #34318, #74673 ) ;
#11824=DIRECTION ( 'NONE',  ( 0.7071067811865487940, -0.7071067811865463515, 0.000000000000000000 ) ) ;
#11825=VECTOR ( 'NONE', #109459, 1000.000000000000000 ) ;
#11826=VECTOR ( 'NONE', #41737, 1000.000000000000000 ) ;
#11828=VECTOR ( 'NONE', #8562, 1000.000000000000000 ) ;
#11830=CARTESIAN_POINT ( 'NONE',  ( -47.99451991528749062, 28.92564299267971251, 4.000000000000000000 ) ) ;
#11831=FACE_BOUND ( 'NONE', #36851, .T. ) ;
#11832=EDGE_CURVE ( 'NONE', #71992, #39593, #43530, .T. ) ;
#11833=LINE ( 'NONE', #13970, #22480 ) ;
#11834=FACE_OUTER_BOUND ( 'NONE', #58370, .T. ) ;
#11835=FACE_OUTER_BOUND ( 'NONE', #106827, .T. ) ;
#11838=CARTESIAN_POINT ( 'NONE',  ( -32.99451991528749062, 28.92564299267960948, 4.000000000000000000 ) ) ;
#11839=VERTEX_POINT ( 'NONE', #41376 ) ;
#11840=ORIENTED_EDGE ( 'NONE', *, *, #19624, .T. ) ;
#11842=ORIENTED_EDGE ( 'NONE', *, *, #82349, .T. ) ;
#11843=DIRECTION ( 'NONE',  ( -1.000000000000000000, 0.000000000000000000, 0.000000000000000000 ) ) ;
#11844=AXIS2_PLACEMENT_3D ( 'NONE', #133135, #44723, #108632 ) ;
#11845=DIRECTION ( 'NONE',  ( -0.000000000000000000, -0.3543493200069152693, 0.9351131265310292928 ) ) ;
#11846=ORIENTED_EDGE ( 'NONE', *, *, #27965, .T. ) ;
#11848=VECTOR ( 'NONE', #955, 999.9999999999998863 ) ;
#11849=CARTESIAN_POINT ( 'NONE',  ( 19.51058707530271974, 22.22500000000000142, 25.62767885193487771 ) ) ;
#11850=DIRECTION ( 'NONE',  ( -0.7071067811865487940, 0.7071067811865463515, 0.000000000000000000 ) ) ;
#11851=VECTOR ( 'NONE', #70881, 1000.000000000000227 ) ;
#11852=CARTESIAN_POINT ( 'NONE',  ( -24.64327148205084583, 5.259292476615665457, 4.831541298974430632 ) ) ;
#11853=PLANE ( 'NONE',  #133851 ) ;
#11854=FACE_OUTER_BOUND ( 'NONE', #114008, .T. ) ;
#11856=DIRECTION ( 'NONE',  ( -0.3543493200069162685, -0.000000000000000000, -0.9351131265310288487 ) ) ;
#11857=DIRECTION ( 'NONE',  ( 0.7071067811865487940, 0.7071067811865463515, 0.000000000000000000 ) ) ;
#11858=VERTEX_POINT ( 'NONE', #97152 ) ;
#11859=VERTEX_POINT ( 'NONE', #42839 ) ;
#11861=DIRECTION ( 'NONE',  ( 0.7071067811865487940, 0.7071067811865463515, 0.000000000000000000 ) ) ;
#11862=DIRECTION ( 'NONE',  ( -0.6830127018922181881, 0.6830127018922202975, -0.2588190451025214056 ) ) ;
#11863=ORIENTED_EDGE ( 'NONE', *, *, #74609, .T. ) ;
#11864=ORIENTED_EDGE ( 'NONE', *, *, #96256, .F. ) ;
#11865=EDGE_LOOP ( 'NONE', ( #62040, #24294, #115358, #63078 ) ) ;
#11866=AXIS2_PLACEMENT_3D ( 'NONE', #44249, #24607, #47147 ) ;
#11867=ADVANCED_FACE ( 'NONE', ( #76167 ), #131984, .F. ) ;
#11869=VERTEX_POINT ( 'NONE', #108747 ) ;
#11870=CARTESIAN_POINT ( 'NONE',  ( 13.82816939922344091, -5.240707523384225297, 4.000000000000000000 ) ) ;
#11871=DIRECTION ( 'NONE',  ( -0.7071067811865487940, 0.7071067811865463515, 0.000000000000000000 ) ) ;
#11872=EDGE_CURVE ( 'NONE', #83353, #16402, #20324, .T. ) ;
#11876=EDGE_CURVE ( 'NONE', #42560, #60723, #141413, .T. ) ;
#11877=EDGE_LOOP ( 'NONE', ( #139918, #132953, #90025, #117985 ) ) ;
#11879=EDGE_CURVE ( 'NONE', #129514, #46484, #118940, .T. ) ;
#11880=CARTESIAN_POINT ( 'NONE',  ( -20.99999999999985079, -13.44781430457069149, 5.000000000000000000 ) ) ;
#11881=VECTOR ( 'NONE', #63900, 1000.000000000000000 ) ;
#11882=CARTESIAN_POINT ( 'NONE',  ( -2.510786437626908008, -27.52281430457053446, 5.000000000000000000 ) ) ;
#11883=LINE ( 'NONE', #1697, #5421 ) ;
#11884=ORIENTED_EDGE ( 'NONE', *, *, #25740, .F. ) ;
#11885=VECTOR ( 'NONE', #6017, 1000.000000000000000 ) ;
#11886=EDGE_LOOP ( 'NONE', ( #79045, #95484, #55603, #46154 ) ) ;
#11887=ADVANCED_FACE ( 'NONE', ( #32670 ), #86338, .F. ) ;
#11889=DIRECTION ( 'NONE',  ( -0.000000000000000000, -0.3543493200069152693, 0.9351131265310292928 ) ) ;
#11890=DIRECTION ( 'NONE',  ( -0.000000000000000000, 0.000000000000000000, 1.000000000000000000 ) ) ;
#11891=EDGE_LOOP ( 'NONE', ( #117432, #27505, #93429, #4531 ) ) ;
#11892=PLANE ( 'NONE',  #131231 ) ;
#11894=ADVANCED_FACE ( 'NONE', ( #75458 ), #54439, .T. ) ;
#11895=VECTOR ( 'NONE', #109339, 1000.000000000000000 ) ;
#11896=CARTESIAN_POINT ( 'NONE',  ( 5.994519915287488843, 28.92564299267942118, 4.000000000000000000 ) ) ;
#11897=FACE_OUTER_BOUND ( 'NONE', #28070, .T. ) ;
#11902=CARTESIAN_POINT ( 'NONE',  ( -30.18398860626900060, 28.73617430169808173, 5.000000000000000000 ) ) ;
#11903=EDGE_CURVE ( 'NONE', #135734, #106183, #76908, .T. ) ;
#11904=LINE ( 'NONE', #14046, #35518 ) ;
#11906=ADVANCED_FACE ( 'NONE', ( #29777 ), #53715, .T. ) ;
#11907=ORIENTED_EDGE ( 'NONE', *, *, #112687, .F. ) ;
#11908=DIRECTION ( 'NONE',  ( -0.7071067811865486830, -0.7071067811865464625, 0.000000000000000000 ) ) ;
#11909=ORIENTED_EDGE ( 'NONE', *, *, #97449, .F. ) ;
#11911=DIRECTION ( 'NONE',  ( 0.6830127018922181881, 0.6830127018922202975, -0.2588190451025214056 ) ) ;
#11912=DIRECTION ( 'NONE',  ( 0.7071067811865486830, -0.7071067811865464625, -0.000000000000000000 ) ) ;
#11913=EDGE_CURVE ( 'NONE', #84298, #15918, #98613, .T. ) ;
#11914=CYLINDRICAL_SURFACE ( 'NONE', #93662, 0.5000000000000004441 ) ;
#11915=PLANE ( 'NONE',  #57561 ) ;
#11917=CARTESIAN_POINT ( 'NONE',  ( 23.52487387214939574, 14.25929247661557042, 9.797011795316691973 ) ) ;
#11918=LINE ( 'NONE', #133035, #120583 ) ;
#11919=DIRECTION ( 'NONE',  ( 0.7071067811865487940, -0.7071067811865463515, 0.000000000000000000 ) ) ;
#11921=CARTESIAN_POINT ( 'NONE',  ( -4.499999999999968914, 16.08746187583908949, 4.000000000000000000 ) ) ;
#11922=CARTESIAN_POINT ( 'NONE',  ( -48.48921356237309510, -27.52281430457089328, 5.000000000000000000 ) ) ;
#11923=AXIS2_PLACEMENT_3D ( 'NONE', #81675, #6179, #138899 ) ;
#11924=CARTESIAN_POINT ( 'NONE',  ( 23.99999999999983302, -5.527737879153171718, -7.983877177622427546 ) ) ;
#11926=CARTESIAN_POINT ( 'NONE',  ( 6.489213562373093325, -27.52281430457059841, 5.000000000000000000 ) ) ;
#11927=VECTOR ( 'NONE', #103173, 999.9999999999998863 ) ;
#11928=AXIS2_PLACEMENT_3D ( 'NONE', #125802, #138821, #116336 ) ;
#11932=ORIENTED_EDGE ( 'NONE', *, *, #9508, .T. ) ;
#11933=EDGE_CURVE ( 'NONE', #6993, #136433, #96441, .T. ) ;
#11934=EDGE_LOOP ( 'NONE', ( #104819, #125726, #19535, #74727 ) ) ;
#11935=VECTOR ( 'NONE', #100567, 1000.000000000000000 ) ;
#11937=VECTOR ( 'NONE', #24597, 1000.000000000000000 ) ;
#11939=VECTOR ( 'NONE', #14322, 1000.000000000000000 ) ;
#11941=CARTESIAN_POINT ( 'NONE',  ( -38.99451991528749062, 28.92564299267965211, 4.000000000000000000 ) ) ;
#11942=CARTESIAN_POINT ( 'NONE',  ( -5.510786437626906675, -27.52281430457051314, 5.000000000000000000 ) ) ;
#11945=CARTESIAN_POINT ( 'NONE',  ( 34.92499999999998295, -21.72500000000000142, 5.000000000000000000 ) ) ;
#11946=ORIENTED_EDGE ( 'NONE', *, *, #118742, .T. ) ;
#11947=ORIENTED_EDGE ( 'NONE', *, *, #72348, .T. ) ;
#11948=DIRECTION ( 'NONE',  ( 0.7071067811865487940, -0.7071067811865463515, 0.000000000000000000 ) ) ;
#11949=DIRECTION ( 'NONE',  ( -0.6830127018922181881, 0.6830127018922202975, -0.2588190451025214056 ) ) ;
#11951=LINE ( 'NONE', #1063, #35805 ) ;
#11952=EDGE_CURVE ( 'NONE', #20334, #24733, #100768, .T. ) ;
#11953=CARTESIAN_POINT ( 'NONE',  ( 20.99999999999985079, -15.41253812416059787, 4.000000000000000000 ) ) ;
#11955=LINE ( 'NONE', #33752, #90294 ) ;
#11956=FACE_OUTER_BOUND ( 'NONE', #10769, .T. ) ;
#11957=ORIENTED_EDGE ( 'NONE', *, *, #86200, .T. ) ;
#11959=DIRECTION ( 'NONE',  ( -0.7071067811865487940, 0.7071067811865463515, -0.000000000000000000 ) ) ;
#11960=EDGE_CURVE ( 'NONE', #44265, #109300, #134858, .T. ) ;
#11961=PLANE ( 'NONE',  #87966 ) ;
#11962=CARTESIAN_POINT ( 'NONE',  ( 5.292893218813427225, -0.7407075233842735917, 5.000000000000000000 ) ) ;
#11963=ORIENTED_EDGE ( 'NONE', *, *, #14981, .F. ) ;
#11964=AXIS2_PLACEMENT_3D ( 'NONE', #81970, #4293, #101530 ) ;
#11965=CARTESIAN_POINT ( 'NONE',  ( 39.48921356237310221, -27.52281430457082934, 5.000000000000000000 ) ) ;
#11966=ORIENTED_EDGE ( 'NONE', *, *, #107722, .T. ) ;
#11967=VECTOR ( 'NONE', #110420, 1000.000000000000227 ) ;
#11969=EDGE_CURVE ( 'NONE', #95196, #78216, #110193, .T. ) ;
#11970=DIRECTION ( 'NONE',  ( -0.7071067811865486830, 0.7071067811865464625, 0.000000000000000000 ) ) ;
#11973=ORIENTED_EDGE ( 'NONE', *, *, #4533, .T. ) ;
#11974=VECTOR ( 'NONE', #18535, 1000.000000000000000 ) ;
#11976=CARTESIAN_POINT ( 'NONE',  ( -34.75611968250420603, -0.1870657452926316466, 4.955485411084897152 ) ) ;
#11977=DIRECTION ( 'NONE',  ( -0.000000000000000000, 0.3543493200069153248, 0.9351131265310292928 ) ) ;
#11978=ADVANCED_FACE ( 'NONE', ( #22461 ), #45705, .F. ) ;
#11979=LINE ( 'NONE', #67851, #120296 ) ;
#11980=ORIENTED_EDGE ( 'NONE', *, *, #125128, .F. ) ;
#11981=DIRECTION ( 'NONE',  ( -0.000000000000000000, 0.3543493200069153248, 0.9351131265310292928 ) ) ;
#11984=VECTOR ( 'NONE', #37933, 999.9999999999998863 ) ;
#11985=PLANE ( 'NONE',  #22894 ) ;
#11986=EDGE_LOOP ( 'NONE', ( #75286, #91244, #23647 ) ) ;
#11990=DIRECTION ( 'NONE',  ( 0.6830127018922181881, 0.6830127018922202975, -0.2588190451025214056 ) ) ;
#11991=CARTESIAN_POINT ( 'NONE',  ( 27.79333936457828358, 21.75929247661549226, 4.998822639870708073 ) ) ;
#11992=VECTOR ( 'NONE', #95617, 1000.000000000000227 ) ;
#11994=CARTESIAN_POINT ( 'NONE',  ( -12.48921356237309155, -27.52281430457064104, 5.000000000000000000 ) ) ;
#11995=ORIENTED_EDGE ( 'NONE', *, *, #102741, .T. ) ;
#11996=ORIENTED_EDGE ( 'NONE', *, *, #19289, .F. ) ;
#11997=VECTOR ( 'NONE', #86320, 1000.000000000000000 ) ;
#12000=ORIENTED_EDGE ( 'NONE', *, *, #76231, .F. ) ;
#12001=EDGE_CURVE ( 'NONE', #62749, #93258, #66715, .T. ) ;
#12002=DIRECTION ( 'NONE',  ( -0.7071067811865487940, 0.7071067811865463515, 0.000000000000000000 ) ) ;
#12003=CARTESIAN_POINT ( 'NONE',  ( 3.005480084712505828, 28.92564299267936079, 4.000000000000000000 ) ) ;
#12004=FACE_OUTER_BOUND ( 'NONE', #87774, .T. ) ;
#12005=VECTOR ( 'NONE', #6701, 1000.000000000000000 ) ;
#12006=ORIENTED_EDGE ( 'NONE', *, *, #37144, .F. ) ;
#12007=FACE_BOUND ( 'NONE', #105330, .T. ) ;
#12008=EDGE_CURVE ( 'NONE', #103350, #21017, #91344, .T. ) ;
#12009=LINE ( 'NONE', #411, #91833 ) ;
#12010=DIRECTION ( 'NONE',  ( 0.6830127018922180770, -0.6830127018922204085, -0.2588190451025213501 ) ) ;
#12011=PLANE ( 'NONE',  #6527 ) ;
#12013=PLANE ( 'NONE',  #31837 ) ;
#12015=DIRECTION ( 'NONE',  ( -0.7071067811865486830, -0.7071067811865464625, -0.000000000000000000 ) ) ;
#12017=ORIENTED_EDGE ( 'NONE', *, *, #71649, .T. ) ;
#12018=ORIENTED_EDGE ( 'NONE', *, *, #64508, .F. ) ;
#12020=ORIENTED_EDGE ( 'NONE', *, *, #24534, .T. ) ;
#12022=VERTEX_POINT ( 'NONE', #35553 ) ;
#12023=FACE_OUTER_BOUND ( 'NONE', #83363, .T. ) ;
#12024=AXIS2_PLACEMENT_3D ( 'NONE', #40831, #117634, #51000 ) ;
#12026=AXIS2_PLACEMENT_3D ( 'NONE', #13060, #57334, #80503 ) ;
#12027=EDGE_CURVE ( 'NONE', #57842, #52361, #78310, .T. ) ;
#12029=VECTOR ( 'NONE', #77008, 1000.000000000000000 ) ;
#12030=AXIS2_PLACEMENT_3D ( 'NONE', #105282, #50922, #14713 ) ;
#12031=PLANE ( 'NONE',  #54048 ) ;
#12032=EDGE_LOOP ( 'NONE', ( #140684, #102826, #36079, #103101 ) ) ;
#12034=CARTESIAN_POINT ( 'NONE',  ( 27.29974487139158512, -27.71228299555225405, 4.000000000000000000 ) ) ;
#12036=PLANE ( 'NONE',  #59680 ) ;
#12037=LINE ( 'NONE', #68598, #49701 ) ;
#12038=FACE_OUTER_BOUND ( 'NONE', #99960, .T. ) ;
#12039=AXIS2_PLACEMENT_3D ( 'NONE', #99690, #75132, #32321 ) ;
#12042=FACE_OUTER_BOUND ( 'NONE', #120090, .T. ) ;
#12044=CARTESIAN_POINT ( 'NONE',  ( 0.7071067811865450192, -3.740707523384246613, 5.000000000000000000 ) ) ;
#12045=DIRECTION ( 'NONE',  ( -0.6830127018922181881, 0.6830127018922202975, -0.2588190451025214056 ) ) ;
#12046=ORIENTED_EDGE ( 'NONE', *, *, #42551, .F. ) ;
#12047=ORIENTED_EDGE ( 'NONE', *, *, #100318, .T. ) ;
#12048=ORIENTED_EDGE ( 'NONE', *, *, #62326, .F. ) ;
#12050=EDGE_LOOP ( 'NONE', ( #16997, #95294, #9301, #128433 ) ) ;
#12051=DIRECTION ( 'NONE',  ( 0.7071067811865486830, -0.7071067811865464625, -0.000000000000000000 ) ) ;
#12056=EDGE_CURVE ( 'NONE', #7217, #51414, #68190, .T. ) ;
#12058=EDGE_LOOP ( 'NONE', ( #15203, #61854, #91197, #21249 ) ) ;
#12059=LINE ( 'NONE', #56347, #11719 ) ;
#12060=PLANE ( 'NONE',  #107166 ) ;
#12061=ORIENTED_EDGE ( 'NONE', *, *, #39190, .F. ) ;
#12062=EDGE_CURVE ( 'NONE', #31236, #135328, #25331, .T. ) ;
#12063=CARTESIAN_POINT ( 'NONE',  ( 24.70710678118637205, 20.25929247661550647, 5.000000000000000000 ) ) ;
#12065=LINE ( 'NONE', #1177, #103059 ) ;
#12066=ORIENTED_EDGE ( 'NONE', *, *, #23611, .T. ) ;
#12067=VECTOR ( 'NONE', #16657, 1000.000000000000114 ) ;
#12068=CARTESIAN_POINT ( 'NONE',  ( 22.22674160717820513, -11.24070752338415780, 18.24660765846987331 ) ) ;
#12069=ORIENTED_EDGE ( 'NONE', *, *, #20418, .F. ) ;
#12070=VECTOR ( 'NONE', #131181, 1000.000000000000000 ) ;
#12072=EDGE_LOOP ( 'NONE', ( #142374, #122576, #118254, #56799 ) ) ;
#12074=DIRECTION ( 'NONE',  ( 1.000000000000000000, 0.000000000000000000, 0.000000000000000000 ) ) ;
#12075=EDGE_CURVE ( 'NONE', #37853, #142351, #34102, .T. ) ;
#12076=LINE ( 'NONE', #111389, #97182 ) ;
#12077=EDGE_CURVE ( 'NONE', #132053, #42748, #68880, .T. ) ;
#12078=DIRECTION ( 'NONE',  ( 0.7071067811865486830, -0.7071067811865464625, -0.000000000000000000 ) ) ;
#12080=VECTOR ( 'NONE', #99390, 1000.000000000000000 ) ;
#12081=CARTESIAN_POINT ( 'NONE',  ( -72.18398860626899705, 28.73617430169837661, 5.000000000000000000 ) ) ;
#12082=EDGE_CURVE ( 'NONE', #15337, #28681, #14585, .T. ) ;
#12084=LINE ( 'NONE', #1882, #16059 ) ;
#12085=LINE ( 'NONE', #25827, #99271 ) ;
#12086=DIRECTION ( 'NONE',  ( -0.3543493200069162685, -0.000000000000000000, -0.9351131265310288487 ) ) ;
#12087=ORIENTED_EDGE ( 'NONE', *, *, #75077, .F. ) ;
#12088=ORIENTED_EDGE ( 'NONE', *, *, #56137, .T. ) ;
#12092=DIRECTION ( 'NONE',  ( -0.6830127018922180770, -0.6830127018922204085, -0.2588190451025213501 ) ) ;
#12093=EDGE_CURVE ( 'NONE', #108226, #130681, #90616, .T. ) ;
#12094=AXIS2_PLACEMENT_3D ( 'NONE', #33225, #99862, #525 ) ;
#12095=LINE ( 'NONE', #142630, #142282 ) ;
#12096=CARTESIAN_POINT ( 'NONE',  ( 38.99451991528749062, 28.92564299267965211, 4.000000000000000000 ) ) ;
#12097=DIRECTION ( 'NONE',  ( 1.000000000000000000, 0.000000000000000000, 0.000000000000000000 ) ) ;
#12098=LINE ( 'NONE', #1209, #39124 ) ;
#12100=LINE ( 'NONE', #109991, #97278 ) ;
#12101=FACE_OUTER_BOUND ( 'NONE', #51698, .T. ) ;
#12103=CARTESIAN_POINT ( 'NONE',  ( 0.000000000000000000, 0.000000000000000000, 5.000000000000000000 ) ) ;
#12104=EDGE_CURVE ( 'NONE', #12281, #6181, #132722, .T. ) ;
#12105=AXIS2_PLACEMENT_3D ( 'NONE', #138354, #14436, #102880 ) ;
#12108=ORIENTED_EDGE ( 'NONE', *, *, #88850, .F. ) ;
#12109=DIRECTION ( 'NONE',  ( -0.7071067811865487940, -0.7071067811865463515, -0.000000000000000000 ) ) ;
#12110=CARTESIAN_POINT ( 'NONE',  ( 18.71230993966015532, -21.73547319004781286, 4.999917730833664642 ) ) ;
#12111=ORIENTED_EDGE ( 'NONE', *, *, #116484, .F. ) ;
#12112=PLANE ( 'NONE',  #87996 ) ;
#12113=FACE_OUTER_BOUND ( 'NONE', #21352, .T. ) ;
#12115=LINE ( 'NONE', #87553, #78635 ) ;
#12116=VECTOR ( 'NONE', #119641, 1000.000000000000000 ) ;
#12117=ORIENTED_EDGE ( 'NONE', *, *, #125536, .T. ) ;
#12118=LINE ( 'NONE', #56402, #130148 ) ;
#12119=VERTEX_POINT ( 'NONE', #36237 ) ;
#12121=EDGE_CURVE ( 'NONE', #102027, #123748, #110893, .T. ) ;
#12123=LINE ( 'NONE', #59255, #1896 ) ;
#12124=ORIENTED_EDGE ( 'NONE', *, *, #141170, .T. ) ;
#12125=CARTESIAN_POINT ( 'NONE',  ( -12.48921356237309155, -27.52281430457064104, 5.000000000000000000 ) ) ;
#12126=FACE_OUTER_BOUND ( 'NONE', #40416, .T. ) ;
#12127=DIRECTION ( 'NONE',  ( -0.000000000000000000, -0.3543493200069152693, 0.9351131265310292928 ) ) ;
#12130=VECTOR ( 'NONE', #49943, 1000.000000000000000 ) ;
#12131=VECTOR ( 'NONE', #81117, 1000.000000000000000 ) ;
#12132=AXIS2_PLACEMENT_3D ( 'NONE', #92980, #69840, #3781 ) ;
#12133=LINE ( 'NONE', #131074, #134640 ) ;
#12134=CARTESIAN_POINT ( 'NONE',  ( 25.49999999999982236, 0.4311230773921849169, 4.000000000000000000 ) ) ;
#12135=ORIENTED_EDGE ( 'NONE', *, *, #127473, .T. ) ;
#12136=ORIENTED_EDGE ( 'NONE', *, *, #12296, .F. ) ;
#12137=VECTOR ( 'NONE', #14919, 1000.000000000000000 ) ;
#12140=ORIENTED_EDGE ( 'NONE', *, *, #36199, .T. ) ;
#12143=CARTESIAN_POINT ( 'NONE',  ( -9.707106781186475075, -0.7407075233842735917, 5.000000000000000000 ) ) ;
#12144=CARTESIAN_POINT ( 'NONE',  ( 26.99999999999981171, 1.552185695429152856, 5.000000000000000000 ) ) ;
#12145=VECTOR ( 'NONE', #127731, 1000.000000000000000 ) ;
#12147=VECTOR ( 'NONE', #122683, 1000.000000000000000 ) ;
#12148=PLANE ( 'NONE',  #140496 ) ;
#12150=DIRECTION ( 'NONE',  ( 0.7071067811865486830, -0.7071067811865464625, -0.000000000000000000 ) ) ;
#12152=FACE_OUTER_BOUND ( 'NONE', #39125, .T. ) ;
#12153=CARTESIAN_POINT ( 'NONE',  ( 23.35681257248248954, -20.24070752338406365, 21.22881796311218139 ) ) ;
#12154=EDGE_CURVE ( 'NONE', #99775, #57637, #92725, .T. ) ;
#12155=LINE ( 'NONE', #99143, #128131 ) ;
#12156=CARTESIAN_POINT ( 'NONE',  ( 21.48921356237309155, -27.52281430457070499, 5.000000000000000000 ) ) ;
#12158=CARTESIAN_POINT ( 'NONE',  ( -33.48921356237309510, -27.52281430457078670, 5.000000000000000000 ) ) ;
#12160=DIRECTION ( 'NONE',  ( -0.7071067811865487940, 0.7071067811865463515, 0.000000000000000000 ) ) ;
#12163=VERTEX_POINT ( 'NONE', #128240 ) ;
#12165=VERTEX_POINT ( 'NONE', #136962 ) ;
#12167=VECTOR ( 'NONE', #6018, 1000.000000000000000 ) ;
#12168=VERTEX_POINT ( 'NONE', #104303 ) ;
#12170=LINE ( 'NONE', #69440, #36354 ) ;
#12171=LINE ( 'NONE', #111489, #22511 ) ;
#12175=CARTESIAN_POINT ( 'NONE',  ( -38.99451991528749062, 28.92564299267965211, 4.000000000000000000 ) ) ;
#12176=VECTOR ( 'NONE', #105462, 999.9999999999998863 ) ;
#12177=DIRECTION ( 'NONE',  ( 0.7071067811865486830, -0.7071067811865464625, -0.000000000000000000 ) ) ;
#12179=ORIENTED_EDGE ( 'NONE', *, *, #61205, .T. ) ;
#12182=DIRECTION ( 'NONE',  ( -0.000000000000000000, -0.3543493200069152693, 0.9351131265310292928 ) ) ;
#12183=CARTESIAN_POINT ( 'NONE',  ( -34.92500000000001137, 11.81665438641030441, 4.500000000000000888 ) ) ;
#12184=ORIENTED_EDGE ( 'NONE', *, *, #137673, .F. ) ;
#12185=EDGE_LOOP ( 'NONE', ( #73994, #101275, #41388, #111253 ) ) ;
#12186=EDGE_CURVE ( 'NONE', #70620, #132165, #14471, .T. ) ;
#12187=LINE ( 'NONE', #11448, #46977 ) ;
#12188=EDGE_CURVE ( 'NONE', #136794, #2587, #69597, .T. ) ;
#12191=DIRECTION ( 'NONE',  ( 0.7071067811865486830, -0.7071067811865464625, -0.000000000000000000 ) ) ;
#12193=LINE ( 'NONE', #35426, #108914 ) ;
#12194=DIRECTION ( 'NONE',  ( -0.7071067811865486830, 0.7071067811865464625, 0.000000000000000000 ) ) ;
#12195=EDGE_LOOP ( 'NONE', ( #108792, #21968, #101512, #140783 ) ) ;
#12197=ORIENTED_EDGE ( 'NONE', *, *, #104535, .F. ) ;
#12198=DIRECTION ( 'NONE',  ( 0.000000000000000000, -1.000000000000000000, 0.000000000000000000 ) ) ;
#12199=ORIENTED_EDGE ( 'NONE', *, *, #22503, .T. ) ;
#12202=EDGE_CURVE ( 'NONE', #48357, #89870, #94153, .T. ) ;
#12203=CARTESIAN_POINT ( 'NONE',  ( -24.18398860626899705, 28.73617430169804265, 5.000000000000000000 ) ) ;
#12204=ORIENTED_EDGE ( 'NONE', *, *, #33086, .T. ) ;
#12205=CARTESIAN_POINT ( 'NONE',  ( -4.171830600776436526, -5.240707523384232402, 4.000000000000000000 ) ) ;
#12206=DIRECTION ( 'NONE',  ( -0.6830127018922181881, 0.6830127018922202975, -0.2588190451025214056 ) ) ;
#12207=LINE ( 'NONE', #76055, #55344 ) ;
#12208=CARTESIAN_POINT ( 'NONE',  ( -26.99999999999981171, -10.44781430457072702, 5.000000000000000000 ) ) ;
#12209=VERTEX_POINT ( 'NONE', #116632 ) ;
#12211=VERTEX_POINT ( 'NONE', #81172 ) ;
#12213=VERTEX_POINT ( 'NONE', #136236 ) ;
#12215=VERTEX_POINT ( 'NONE', #125381 ) ;
#12216=DIRECTION ( 'NONE',  ( -0.7071067811865486830, -0.7071067811865464625, 0.000000000000000000 ) ) ;
#12217=ORIENTED_EDGE ( 'NONE', *, *, #93750, .T. ) ;
#12218=VERTEX_POINT ( 'NONE', #114478 ) ;
#12219=VECTOR ( 'NONE', #81188, 1000.000000000000227 ) ;
#12220=EDGE_LOOP ( 'NONE', ( #92663, #5804, #77285, #86962 ) ) ;
#12221=FACE_OUTER_BOUND ( 'NONE', #33807, .T. ) ;
#12222=EDGE_CURVE ( 'NONE', #49377, #114574, #126101, .T. ) ;
#12223=DIRECTION ( 'NONE',  ( 0.7071067811865487940, 0.7071067811865463515, 0.000000000000000000 ) ) ;
#12224=CARTESIAN_POINT ( 'NONE',  ( 22.37177410554622980, -1.784312229707115893, 4.000000000000000000 ) ) ;
#12227=EDGE_CURVE ( 'NONE', #77399, #32218, #54418, .T. ) ;
#12228=CARTESIAN_POINT ( 'NONE',  ( -23.20710678118638626, -14.24070752338412937, 5.000000000000000000 ) ) ;
#12229=DIRECTION ( 'NONE',  ( -0.000000000000000000, -0.3543493200069152693, 0.9351131265310292928 ) ) ;
#12230=VECTOR ( 'NONE', #18307, 1000.000000000000000 ) ;
#12231=CARTESIAN_POINT ( 'NONE',  ( 8.999999999999937828, -8.151047557385062703, -8.977947279169821826 ) ) ;
#12232=ADVANCED_FACE ( 'NONE', ( #17315 ), #31074, .F. ) ;
#12233=AXIS2_PLACEMENT_3D ( 'NONE', #28516, #53843, #8824 ) ;
#12234=EDGE_CURVE ( 'NONE', #45041, #118319, #96975, .T. ) ;
#12235=VECTOR ( 'NONE', #11856, 1000.000000000000227 ) ;
#12237=ORIENTED_EDGE ( 'NONE', *, *, #71081, .T. ) ;
#12239=DIRECTION ( 'NONE',  ( 1.000000000000000000, 0.000000000000000000, 0.000000000000000000 ) ) ;
#12240=CARTESIAN_POINT ( 'NONE',  ( -10.49999999999991829, 0.4497235411627317769, -5.599840258123564674 ) ) ;
#12241=ORIENTED_EDGE ( 'NONE', *, *, #70849, .T. ) ;
#12242=ORIENTED_EDGE ( 'NONE', *, *, #131938, .T. ) ;
#12243=ORIENTED_EDGE ( 'NONE', *, *, #54482, .F. ) ;
#12244=VECTOR ( 'NONE', #70161, 999.9999999999998863 ) ;
#12245=CARTESIAN_POINT ( 'NONE',  ( 60.18398860626900415, 28.73617430169829490, 5.000000000000000000 ) ) ;
#12246=ORIENTED_EDGE ( 'NONE', *, *, #52715, .T. ) ;
#12248=LINE ( 'NONE', #100708, #60672 ) ;
#12249=CARTESIAN_POINT ( 'NONE',  ( -42.18398860626899705, 28.73617430169816700, 5.000000000000000000 ) ) ;
#12250=CARTESIAN_POINT ( 'NONE',  ( -34.92500000000001137, -7.285322628117655519, -6.182564397582745563 ) ) ;
#12251=EDGE_CURVE ( 'NONE', #53667, #76579, #10008, .T. ) ;
#12252=LINE ( 'NONE', #102856, #141183 ) ;
#12253=ADVANCED_FACE ( 'NONE', ( #84721 ), #107866, .F. ) ;
#12254=LINE ( 'NONE', #34036, #37099 ) ;
#12255=ORIENTED_EDGE ( 'NONE', *, *, #87596, .F. ) ;
#12256=CARTESIAN_POINT ( 'NONE',  ( -25.41009064519816718, 9.759292476615621936, 11.28811694763772877 ) ) ;
#12257=EDGE_LOOP ( 'NONE', ( #87094, #140643, #107802, #111179 ) ) ;
#12258=CARTESIAN_POINT ( 'NONE',  ( 14.11732500641695509, -0.1862019290248694003, 4.000000000000000000 ) ) ;
#12263=EDGE_CURVE ( 'NONE', #139982, #58396, #119457, .T. ) ;
#12264=LINE ( 'NONE', #68138, #22784 ) ;
#12265=CARTESIAN_POINT ( 'NONE',  ( -34.42500000000001137, -6.022814304570508703, 5.000000000000000000 ) ) ;
#12266=ORIENTED_EDGE ( 'NONE', *, *, #124001, .F. ) ;
#12267=DIRECTION ( 'NONE',  ( 0.7071067811865487940, 0.7071067811865463515, 0.000000000000000000 ) ) ;
#12269=ORIENTED_EDGE ( 'NONE', *, *, #90707, .T. ) ;
#12271=LINE ( 'NONE', #10823, #71791 ) ;
#12272=ADVANCED_FACE ( 'NONE', ( #128932 ), #108564, .F. ) ;
#12273=CARTESIAN_POINT ( 'NONE',  ( -32.99451991528749062, 28.92564299267960948, 4.000000000000000000 ) ) ;
#12274=CARTESIAN_POINT ( 'NONE',  ( 2.816011393730999401, 28.73617430169785436, 5.000000000000000000 ) ) ;
#12275=VERTEX_POINT ( 'NONE', #98448 ) ;
#12276=AXIS2_PLACEMENT_3D ( 'NONE', #65052, #110641, #75222 ) ;
#12278=VECTOR ( 'NONE', #101782, 1000.000000000000000 ) ;
#12279=CARTESIAN_POINT ( 'NONE',  ( -24.18398860626899705, 28.73617430169804265, 5.000000000000000000 ) ) ;
#12280=PLANE ( 'NONE',  #23709 ) ;
#12281=VERTEX_POINT ( 'NONE', #87576 ) ;
#12282=CARTESIAN_POINT ( 'NONE',  ( 8.488313940715631389, 6.759292476615645917, 16.35960578974467694 ) ) ;
#12284=DIRECTION ( 'NONE',  ( 0.6830127018922180770, -0.6830127018922204085, -0.2588190451025213501 ) ) ;
#12285=VERTEX_POINT ( 'NONE', #75292 ) ;
#12286=LINE ( 'NONE', #75425, #23210 ) ;
#12287=ORIENTED_EDGE ( 'NONE', *, *, #13794, .F. ) ;
#12288=ORIENTED_EDGE ( 'NONE', *, *, #118638, .T. ) ;
#12289=DIRECTION ( 'NONE',  ( -0.7071067811865487940, 0.7071067811865463515, 0.000000000000000000 ) ) ;
#12290=DIRECTION ( 'NONE',  ( 0.000000000000000000, -1.000000000000000000, 0.000000000000000000 ) ) ;
#12291=ORIENTED_EDGE ( 'NONE', *, *, #73548, .T. ) ;
#12292=CARTESIAN_POINT ( 'NONE',  ( -34.92500000000001137, 8.816654386410331057, 4.500000000000000888 ) ) ;
#12294=CARTESIAN_POINT ( 'NONE',  ( 0.000000000000000000, 8.966399257802175171, 5.000000000000000000 ) ) ;
#12295=LINE ( 'NONE', #25307, #108734 ) ;
#12296=EDGE_CURVE ( 'NONE', #8442, #89327, #63705, .T. ) ;
#12297=DIRECTION ( 'NONE',  ( -0.7071067811865486830, -0.7071067811865464625, 0.000000000000000000 ) ) ;
#12298=AXIS2_PLACEMENT_3D ( 'NONE', #101791, #36539, #114100 ) ;
#12299=LINE ( 'NONE', #134838, #80726 ) ;
#12300=CARTESIAN_POINT ( 'NONE',  ( 41.35681257248237586, -20.24070752338406720, 21.22881796311222047 ) ) ;
#12301=DIRECTION ( 'NONE',  ( -0.7071067811865486830, 0.7071067811865464625, 0.000000000000000000 ) ) ;
#12302=LINE ( 'NONE', #68177, #79597 ) ;
#12303=LINE ( 'NONE', #100754, #25134 ) ;
#12305=CARTESIAN_POINT ( 'NONE',  ( -34.28351269101152354, -22.22500000000000142, 5.243083521430598637 ) ) ;
#12306=AXIS2_PLACEMENT_3D ( 'NONE', #94867, #16604, #3568 ) ;
#12307=LINE ( 'NONE', #136227, #41266 ) ;
#12309=CARTESIAN_POINT ( 'NONE',  ( -34.49999999999975131, -7.912538124160673370, 4.000000000000000000 ) ) ;
#12311=( BOUNDED_CURVE ( )  B_SPLINE_CURVE ( 3, ( #106286, #6961, #43231, #85270 ),
 .UNSPECIFIED., .F., .F. ) 
 B_SPLINE_CURVE_WITH_KNOTS ( ( 4, 4 ),
 ( 1.142100667999822905, 1.182775789206201633 ),
 .UNSPECIFIED. ) 
 CURVE ( )  GEOMETRIC_REPRESENTATION_ITEM ( )  RATIONAL_B_SPLINE_CURVE ( ( 1.000000000000000000, 0.9998621326283523292, 0.9998621326283523292, 1.000000000000000000 ) ) 
 REPRESENTATION_ITEM ( '' )  );
#12312=ORIENTED_EDGE ( 'NONE', *, *, #79764, .T. ) ;
#12314=ORIENTED_EDGE ( 'NONE', *, *, #32548, .T. ) ;
#12316=ORIENTED_EDGE ( 'NONE', *, *, #36552, .T. ) ;
#12319=AXIS2_PLACEMENT_3D ( 'NONE', #115570, #83742, #104736 ) ;
#12321=ORIENTED_EDGE ( 'NONE', *, *, #139992, .F. ) ;
#12323=CARTESIAN_POINT ( 'NONE',  ( 32.99999999999977973, -16.44781430457066662, 5.000000000000000000 ) ) ;
#12324=DIRECTION ( 'NONE',  ( -0.7071067811865486830, 0.7071067811865464625, 0.000000000000000000 ) ) ;
#12325=DIRECTION ( 'NONE',  ( -0.7071067811865486830, -0.7071067811865464625, 0.000000000000000000 ) ) ;
#12326=ORIENTED_EDGE ( 'NONE', *, *, #34263, .F. ) ;
#12327=CARTESIAN_POINT ( 'NONE',  ( 20.24139925780189841, 21.72500000000000853, 5.000000000000000000 ) ) ;
#12328=CARTESIAN_POINT ( 'NONE',  ( 12.79289321881337038, -17.24070752338410273, 5.000000000000000000 ) ) ;
#12329=DIRECTION ( 'NONE',  ( -0.000000000000000000, 0.000000000000000000, 1.000000000000000000 ) ) ;
#12330=VECTOR ( 'NONE', #80146, 1000.000000000000227 ) ;
#12331=CARTESIAN_POINT ( 'NONE',  ( -57.48921356237308800, -27.52281430457095368, 5.000000000000000000 ) ) ;
#12333=CARTESIAN_POINT ( 'NONE',  ( 35.99451991528749772, 28.92564299267963079, 4.000000000000000000 ) ) ;
#12334=LINE ( 'NONE', #34115, #100789 ) ;
#12336=ORIENTED_EDGE ( 'NONE', *, *, #53115, .T. ) ;
#12337=ORIENTED_EDGE ( 'NONE', *, *, #11363, .F. ) ;
#12339=VERTEX_POINT ( 'NONE', #43366 ) ;
#12341=LINE ( 'NONE', #110918, #8458 ) ;
#12342=VECTOR ( 'NONE', #21748, 1000.000000000000000 ) ;
#12343=DIRECTION ( 'NONE',  ( -0.7071067811865486830, -0.7071067811865464625, 0.000000000000000000 ) ) ;
#12344=CARTESIAN_POINT ( 'NONE',  ( -16.49999999999988631, -14.56887692260766087, 4.000000000000000000 ) ) ;
#12345=DIRECTION ( 'NONE',  ( 0.7071067811865486830, -0.7071067811865464625, -0.000000000000000000 ) ) ;
#12346=VECTOR ( 'NONE', #65235, 1000.000000000000000 ) ;
#12348=VERTEX_POINT ( 'NONE', #73843 ) ;
#12349=EDGE_CURVE ( 'NONE', #136794, #39797, #118765, .T. ) ;
#12350=EDGE_LOOP ( 'NONE', ( #84445, #48626, #98553, #110758 ) ) ;
#12351=VECTOR ( 'NONE', #140132, 1000.000000000000227 ) ;
#12353=FACE_OUTER_BOUND ( 'NONE', #59935, .T. ) ;
#12354=ORIENTED_EDGE ( 'NONE', *, *, #83819, .F. ) ;
#12355=EDGE_LOOP ( 'NONE', ( #90303, #142154, #35733, #18536 ) ) ;
#12357=EDGE_CURVE ( 'NONE', #13638, #93212, #18721, .T. ) ;
#12358=VERTEX_POINT ( 'NONE', #109325 ) ;
#12359=LINE ( 'NONE', #134160, #107035 ) ;
#12360=EDGE_CURVE ( 'NONE', #115620, #143546, #41203, .T. ) ;
#12363=EDGE_CURVE ( 'NONE', #43296, #28403, #107173, .T. ) ;
#12364=VECTOR ( 'NONE', #110876, 1000.000000000000000 ) ;
#12367=EDGE_CURVE ( 'NONE', #143444, #11445, #52090, .T. ) ;
#12368=PLANE ( 'NONE',  #20133 ) ;
#12369=ORIENTED_EDGE ( 'NONE', *, *, #95993, .T. ) ;
#12370=VERTEX_POINT ( 'NONE', #12143 ) ;
#12371=VERTEX_POINT ( 'NONE', #89028 ) ;
#12373=EDGE_CURVE ( 'NONE', #110737, #117346, #133246, .T. ) ;
#12375=EDGE_LOOP ( 'NONE', ( #31128, #32761, #14358, #98270 ) ) ;
#12376=CIRCLE ( 'NONE', #142077, 5.968999999999998529 ) ;
#12377=DIRECTION ( 'NONE',  ( -0.000000000000000000, -0.3543493200069152693, 0.9351131265310292928 ) ) ;
#12378=LINE ( 'NONE', #53780, #98849 ) ;
#12379=EDGE_CURVE ( 'NONE', #123460, #26065, #76729, .T. ) ;
#12380=CARTESIAN_POINT ( 'NONE',  ( 29.99999999999979039, 8.587461875839165870, 4.000000000000000000 ) ) ;
#12382=FACE_BOUND ( 'NONE', #55008, .T. ) ;
#12383=EDGE_LOOP ( 'NONE', ( #99512, #139166, #85799 ) ) ;
#12384=CARTESIAN_POINT ( 'NONE',  ( -9.328169399223463998, -21.74070752338406365, 4.000000000000000000 ) ) ;
#12385=LINE ( 'NONE', #45774, #134083 ) ;
#12386=CARTESIAN_POINT ( 'NONE',  ( -2.207106781186522149, -11.24070752338417023, 5.000000000000000000 ) ) ;
#12387=CARTESIAN_POINT ( 'NONE',  ( -9.183988606268997046, 28.73617430169793607, 5.000000000000000000 ) ) ;
#12388=VERTEX_POINT ( 'NONE', #21609 ) ;
#12390=ORIENTED_EDGE ( 'NONE', *, *, #72116, .F. ) ;
#12393=EDGE_LOOP ( 'NONE', ( #95364, #74800, #10690, #12903 ) ) ;
#12396=EDGE_LOOP ( 'NONE', ( #61610, #31871, #40293, #12241 ) ) ;
#12398=FACE_OUTER_BOUND ( 'NONE', #104938, .T. ) ;
#12399=ADVANCED_FACE ( 'NONE', ( #22989 ), #12844, .F. ) ;
#12400=ORIENTED_EDGE ( 'NONE', *, *, #25145, .T. ) ;
#12401=DIRECTION ( 'NONE',  ( 0.7071067811865487940, -0.7071067811865463515, 0.000000000000000000 ) ) ;
#12402=CARTESIAN_POINT ( 'NONE',  ( 3.183988606268992161, 28.73617430169789699, 5.000000000000000000 ) ) ;
#12403=AXIS2_PLACEMENT_3D ( 'NONE', #110033, #45546, #10703 ) ;
#12404=ADVANCED_FACE ( 'NONE', ( #78865 ), #101303, .F. ) ;
#12405=EDGE_CURVE ( 'NONE', #33213, #10686, #88304, .T. ) ;
#12406=LINE ( 'NONE', #77694, #15720 ) ;
#12407=CARTESIAN_POINT ( 'NONE',  ( 27.52400138585429445, 22.03583458319437582, 4.979811245910090278 ) ) ;
#12408=LINE ( 'NONE', #135638, #111917 ) ;
#12409=VERTEX_POINT ( 'NONE', #110024 ) ;
#12411=VECTOR ( 'NONE', #7435, 1000.000000000000000 ) ;
#12412=ORIENTED_EDGE ( 'NONE', *, *, #50669, .F. ) ;
#12413=ORIENTED_EDGE ( 'NONE', *, *, #116729, .F. ) ;
#12414=CARTESIAN_POINT ( 'NONE',  ( -17.99451991528748351, 28.92564299267950645, 4.000000000000000000 ) ) ;
#12415=FACE_OUTER_BOUND ( 'NONE', #81168, .T. ) ;
#12416=EDGE_LOOP ( 'NONE', ( #25831, #110158, #103284, #78631 ) ) ;
#12417=ADVANCED_FACE ( 'NONE', ( #57830 ), #78142, .F. ) ;
#12418=ORIENTED_EDGE ( 'NONE', *, *, #72587, .T. ) ;
#12419=LINE ( 'NONE', #57388, #95285 ) ;
#12420=DIRECTION ( 'NONE',  ( 0.6830127018922181881, 0.6830127018922202975, -0.2588190451025214056 ) ) ;
#12421=EDGE_CURVE ( 'NONE', #42811, #86060, #57124, .T. ) ;
#12424=ORIENTED_EDGE ( 'NONE', *, *, #127901, .T. ) ;
#12425=CARTESIAN_POINT ( 'NONE',  ( -4.998069433178984333, -22.22500000000000142, 4.500000000000000888 ) ) ;
#12426=CARTESIAN_POINT ( 'NONE',  ( 23.55512991947088963, -0.7407075233842735917, 4.307968247157003994 ) ) ;
#12429=VERTEX_POINT ( 'NONE', #90429 ) ;
#12431=DIRECTION ( 'NONE',  ( 0.7071067811865486830, -0.7071067811865464625, -0.000000000000000000 ) ) ;
#12432=EDGE_CURVE ( 'NONE', #68468, #105421, #102023, .T. ) ;
#12433=CARTESIAN_POINT ( 'NONE',  ( -8.816011393731004731, 28.73617430169781173, 5.000000000000000000 ) ) ;
#12434=FACE_OUTER_BOUND ( 'NONE', #43790, .T. ) ;
#12435=DIRECTION ( 'NONE',  ( -0.3543493200069162685, -0.000000000000000000, -0.9351131265310288487 ) ) ;
#12436=DIRECTION ( 'NONE',  ( 0.3543493200069162685, -0.000000000000000000, -0.9351131265310288487 ) ) ;
#12437=ORIENTED_EDGE ( 'NONE', *, *, #59279, .F. ) ;
#12440=CARTESIAN_POINT ( 'NONE',  ( -29.99999999999978328, 2.966399257802232459, 5.000000000000000000 ) ) ;
#12441=ADVANCED_FACE ( 'NONE', ( #32493 ), #34625, .F. ) ;
#12443=CARTESIAN_POINT ( 'NONE',  ( 33.27825451568553206, 8.259292476615634371, 11.78515199841158356 ) ) ;
#12445=EDGE_LOOP ( 'NONE', ( #9388, #113424, #15376, #95714 ) ) ;
#12446=LINE ( 'NONE', #69729, #32030 ) ;
#12447=DIRECTION ( 'NONE',  ( -0.7071067811865486830, -0.7071067811865464625, -0.000000000000000000 ) ) ;
#12449=ORIENTED_EDGE ( 'NONE', *, *, #124592, .T. ) ;
#12450=DIRECTION ( 'NONE',  ( -2.781805975412905890E-17, 0.3543493200069152693, 0.9351131265310292928 ) ) ;
#12452=DIRECTION ( 'NONE',  ( -0.6830127018922180770, -0.6830127018922204085, -0.2588190451025213501 ) ) ;
#12453=DIRECTION ( 'NONE',  ( 0.3543493200069162685, -0.000000000000000000, -0.9351131265310288487 ) ) ;
#12454=EDGE_LOOP ( 'NONE', ( #79200, #13284, #57601, #54642 ) ) ;
#12456=EDGE_LOOP ( 'NONE', ( #77496, #31661, #138133, #139546 ) ) ;
#12457=CARTESIAN_POINT ( 'NONE',  ( -28.17183060077627843, 9.759292476615620160, 4.000000000000000000 ) ) ;
#12459=AXIS2_PLACEMENT_3D ( 'NONE', #51839, #20602, #21341 ) ;
#12460=ORIENTED_EDGE ( 'NONE', *, *, #126042, .F. ) ;
#12461=CARTESIAN_POINT ( 'NONE',  ( -44.99451991528749772, 28.92564299267969474, 4.000000000000000000 ) ) ;
#12462=EDGE_CURVE ( 'NONE', #27078, #8640, #134676, .T. ) ;
#12463=AXIS2_PLACEMENT_3D ( 'NONE', #26053, #24610, #36908 ) ;
#12464=DIRECTION ( 'NONE',  ( 0.6830127018922180770, -0.6830127018922204085, -0.2588190451025213501 ) ) ;
#12465=CARTESIAN_POINT ( 'NONE',  ( -25.17183060077628909, 21.75929247661549581, 4.000000000000000000 ) ) ;
#12466=ORIENTED_EDGE ( 'NONE', *, *, #100476, .T. ) ;
#12467=CARTESIAN_POINT ( 'NONE',  ( -12.18398860626900060, 28.73617430169795739, 5.000000000000000000 ) ) ;
#12468=DIRECTION ( 'NONE',  ( -0.000000000000000000, 0.3543493200069152138, -0.9351131265310292928 ) ) ;
#12469=LINE ( 'NONE', #11018, #758 ) ;
#12470=LINE ( 'NONE', #134273, #74862 ) ;
#12473=DIRECTION ( 'NONE',  ( 0.7071067811865487940, 0.7071067811865463515, 0.000000000000000000 ) ) ;
#12474=ORIENTED_EDGE ( 'NONE', *, *, #140104, .T. ) ;
#12475=VERTEX_POINT ( 'NONE', #46987 ) ;
#12476=EDGE_LOOP ( 'NONE', ( #137015, #35794, #61325, #41176 ) ) ;
#12479=ORIENTED_EDGE ( 'NONE', *, *, #69450, .T. ) ;
#12480=VECTOR ( 'NONE', #79978, 1000.000000000000000 ) ;
#12481=ORIENTED_EDGE ( 'NONE', *, *, #15351, .T. ) ;
#12483=CARTESIAN_POINT ( 'NONE',  ( -34.92500000000001137, 12.31448516125890436, 8.755464546898137357 ) ) ;
#12484=ORIENTED_EDGE ( 'NONE', *, *, #127392, .F. ) ;
#12485=CARTESIAN_POINT ( 'NONE',  ( 0.000000000000000000, 0.000000000000000000, 5.000000000000000000 ) ) ;
#12487=VECTOR ( 'NONE', #116690, 1000.000000000000000 ) ;
#12488=DIRECTION ( 'NONE',  ( -0.6830127018922180770, -0.6830127018922204085, -0.2588190451025213501 ) ) ;
#12489=VECTOR ( 'NONE', #103707, 999.9999999999998863 ) ;
#12493=CARTESIAN_POINT ( 'NONE',  ( -0.005480084712502889671, 28.92564299267938210, 4.000000000000000000 ) ) ;
#12494=CARTESIAN_POINT ( 'NONE',  ( 14.01088028653938089, -22.02621442084248571, 4.990779571109220214 ) ) ;
#12495=PLANE ( 'NONE',  #121330 ) ;
#12497=LINE ( 'NONE', #54604, #114505 ) ;
#12499=LINE ( 'NONE', #56780, #76953 ) ;
#12500=CARTESIAN_POINT ( 'NONE',  ( -6.328169399223485314, -0.7407075233842735917, 4.000000000000000000 ) ) ;
#12501=VECTOR ( 'NONE', #33656, 1000.000000000000000 ) ;
#12503=DIRECTION ( 'NONE',  ( -0.7071067811865486830, 0.7071067811865464625, 0.000000000000000000 ) ) ;
#12504=VECTOR ( 'NONE', #43830, 999.9999999999998863 ) ;
#12505=CARTESIAN_POINT ( 'NONE',  ( -24.15612307739226239, -22.22500000000000853, 4.000000000000000000 ) ) ;
#12506=ORIENTED_EDGE ( 'NONE', *, *, #16087, .T. ) ;
#12507=ORIENTED_EDGE ( 'NONE', *, *, #140064, .T. ) ;
#12509=CARTESIAN_POINT ( 'NONE',  ( 0.000000000000000000, 0.000000000000000000, 5.000000000000000000 ) ) ;
#12510=VECTOR ( 'NONE', #129450, 1000.000000000000000 ) ;
#12511=ORIENTED_EDGE ( 'NONE', *, *, #62865, .F. ) ;
#12512=DIRECTION ( 'NONE',  ( -0.6830127018922181881, 0.6830127018922202975, -0.2588190451025214056 ) ) ;
#12514=VECTOR ( 'NONE', #141323, 1000.000000000000000 ) ;
#12515=EDGE_CURVE ( 'NONE', #89327, #103007, #543, .T. ) ;
#12517=ORIENTED_EDGE ( 'NONE', *, *, #141699, .T. ) ;
#12518=EDGE_CURVE ( 'NONE', #102268, #51675, #34081, .T. ) ;
#12519=CARTESIAN_POINT ( 'NONE',  ( 15.44591897758377286, -1.592173378680614926, 4.204195949441833058 ) ) ;
#12520=ORIENTED_EDGE ( 'NONE', *, *, #20065, .F. ) ;
#12521=VECTOR ( 'NONE', #2815, 999.9999999999998863 ) ;
#12522=CARTESIAN_POINT ( 'NONE',  ( -34.42500000000001137, 0.000000000000000000, 4.500000000000000888 ) ) ;
#12523=CARTESIAN_POINT ( 'NONE',  ( -18.48921356237309510, -27.52281430457068367, 5.000000000000000000 ) ) ;
#12524=EDGE_CURVE ( 'NONE', #89838, #115114, #23749, .T. ) ;
#12526=CARTESIAN_POINT ( 'NONE',  ( 34.92499999999998295, 22.22500000000000142, 4.000000000000000000 ) ) ;
#12527=ADVANCED_FACE ( 'NONE', ( #132550 ), #121611, .T. ) ;
#12528=EDGE_CURVE ( 'NONE', #22434, #94617, #72301, .T. ) ;
#12530=LINE ( 'NONE', #68391, #132754 ) ;
#12531=CARTESIAN_POINT ( 'NONE',  ( -31.11017322888190151, -22.22500000000000497, 4.785647885939355639 ) ) ;
#12532=PLANE ( 'NONE',  #70892 ) ;
#12534=LINE ( 'NONE', #77813, #44044 ) ;
#12535=CARTESIAN_POINT ( 'NONE',  ( -14.28769006033961020, -21.73547319004781286, 4.999917730833664642 ) ) ;
#12536=ADVANCED_FACE ( 'NONE', ( #70158 ), #83131, .T. ) ;
#12537=EDGE_CURVE ( 'NONE', #25811, #77500, #26602, .T. ) ;
#12538=EDGE_LOOP ( 'NONE', ( #72770, #101368, #84208, #65762 ) ) ;
#12539=DIRECTION ( 'NONE',  ( 0.7071067811865487940, 0.7071067811865463515, 0.000000000000000000 ) ) ;
#12541=DIRECTION ( 'NONE',  ( 0.7071067811865487940, 0.7071067811865463515, 0.000000000000000000 ) ) ;
#12542=ADVANCED_FACE ( 'NONE', ( #59269 ), #114317, .F. ) ;
#12543=DIRECTION ( 'NONE',  ( -0.6830127018922180770, -0.6830127018922204085, -0.2588190451025213501 ) ) ;
#12544=FACE_OUTER_BOUND ( 'NONE', #137993, .T. ) ;
#12545=ORIENTED_EDGE ( 'NONE', *, *, #22063, .F. ) ;
#12546=CARTESIAN_POINT ( 'NONE',  ( 78.18398860626899705, 28.73617430169841924, 5.000000000000000000 ) ) ;
#12549=ADVANCED_FACE ( 'NONE', ( #91846 ), #58578, .F. ) ;
#12550=DIRECTION ( 'NONE',  ( -0.7071067811865486830, 0.7071067811865464625, 0.000000000000000000 ) ) ;
#12551=EDGE_LOOP ( 'NONE', ( #39242, #141587, #84820, #142515 ) ) ;
#12552=DIRECTION ( 'NONE',  ( 1.000000000000000000, 0.000000000000000000, 0.000000000000000000 ) ) ;
#12553=DIRECTION ( 'NONE',  ( 0.3543493200069162685, -0.000000000000000000, -0.9351131265310288487 ) ) ;
#12554=DIRECTION ( 'NONE',  ( -0.7071067811865487940, 0.7071067811865463515, 0.000000000000000000 ) ) ;
#12555=DIRECTION ( 'NONE',  ( 0.7071067811865486830, -0.7071067811865464625, -0.000000000000000000 ) ) ;
#12556=FACE_BOUND ( 'NONE', #79977, .T. ) ;
#12557=LINE ( 'NONE', #22691, #135924 ) ;
#12558=CARTESIAN_POINT ( 'NONE',  ( -45.18398860626900415, 28.73617430169818832, 5.000000000000000000 ) ) ;
#12559=FACE_OUTER_BOUND ( 'NONE', #61235, .T. ) ;
#12560=CARTESIAN_POINT ( 'NONE',  ( 48.48921356237309510, -27.52281430457089328, 5.000000000000000000 ) ) ;
#12561=ORIENTED_EDGE ( 'NONE', *, *, #96012, .F. ) ;
#12562=AXIS2_PLACEMENT_3D ( 'NONE', #105308, #115433, #5964 ) ;
#12563=EDGE_CURVE ( 'NONE', #11170, #60604, #38208, .T. ) ;
#12565=ORIENTED_EDGE ( 'NONE', *, *, #113633, .F. ) ;
#12567=VERTEX_POINT ( 'NONE', #36753 ) ;
#12569=ORIENTED_EDGE ( 'NONE', *, *, #38528, .F. ) ;
#12570=PLANE ( 'NONE',  #131010 ) ;
#12571=DIRECTION ( 'NONE',  ( -0.7071067811865486830, -0.7071067811865464625, 0.000000000000000000 ) ) ;
#12572=VECTOR ( 'NONE', #130198, 1000.000000000000000 ) ;
#12573=EDGE_CURVE ( 'NONE', #23940, #60723, #14994, .T. ) ;
#12575=DIRECTION ( 'NONE',  ( -0.000000000000000000, 0.000000000000000000, 1.000000000000000000 ) ) ;
#12576=DIRECTION ( 'NONE',  ( -0.000000000000000000, 0.3543493200069153248, 0.9351131265310292928 ) ) ;
#12577=EDGE_CURVE ( 'NONE', #83408, #11149, #138221, .T. ) ;
#12578=CARTESIAN_POINT ( 'NONE',  ( 59.99451991528749772, 28.92564299267980132, 4.000000000000000000 ) ) ;
#12580=VECTOR ( 'NONE', #80667, 1000.000000000000000 ) ;
#12581=DIRECTION ( 'NONE',  ( -0.7071067811865486830, -0.7071067811865464625, 0.000000000000000000 ) ) ;
#12582=EDGE_CURVE ( 'NONE', #88566, #120007, #126604, .T. ) ;
#12584=CARTESIAN_POINT ( 'NONE',  ( -15.85181644961845748, 17.25929247661554200, 8.802941693769165354 ) ) ;
#12585=EDGE_LOOP ( 'NONE', ( #64684, #79963, #89047, #33999 ) ) ;
#12586=ORIENTED_EDGE ( 'NONE', *, *, #26386, .T. ) ;
#12588=DIRECTION ( 'NONE',  ( 0.7071067811865487940, 0.7071067811865463515, 0.000000000000000000 ) ) ;
#12589=VERTEX_POINT ( 'NONE', #125205 ) ;
#12590=ADVANCED_FACE ( 'NONE', ( #69409 ), #25158, .F. ) ;
#12591=ORIENTED_EDGE ( 'NONE', *, *, #7259, .F. ) ;
#12593=VECTOR ( 'NONE', #96398, 1000.000000000000000 ) ;
#12595=VERTEX_POINT ( 'NONE', #125928 ) ;
#12596=CARTESIAN_POINT ( 'NONE',  ( -6.183988606268994381, 28.73617430169791476, 5.000000000000000000 ) ) ;
#12597=EDGE_CURVE ( 'NONE', #139414, #128406, #70845, .T. ) ;
#12598=AXIS2_PLACEMENT_3D ( 'NONE', #83213, #126689, #71630 ) ;
#12600=VECTOR ( 'NONE', #25212, 1000.000000000000000 ) ;
#12602=VECTOR ( 'NONE', #94803, 999.9999999999998863 ) ;
#12604=ORIENTED_EDGE ( 'NONE', *, *, #69220, .F. ) ;
#12605=EDGE_CURVE ( 'NONE', #81561, #16866, #16407, .T. ) ;
#12606=CARTESIAN_POINT ( 'NONE',  ( -36.48921356237310221, -27.52281430457080802, 5.000000000000000000 ) ) ;
#12608=CARTESIAN_POINT ( 'NONE',  ( -68.99451991528748351, 28.92564299267986172, 4.000000000000000000 ) ) ;
#12609=DIRECTION ( 'NONE',  ( -0.7071067811865486830, 0.7071067811865464625, 0.000000000000000000 ) ) ;
#12610=ORIENTED_EDGE ( 'NONE', *, *, #12709, .T. ) ;
#12611=EDGE_LOOP ( 'NONE', ( #43002, #78438, #38669, #119267 ) ) ;
#12613=CARTESIAN_POINT ( 'NONE',  ( 12.48921356237309155, -27.52281430457064104, 5.000000000000000000 ) ) ;
#12614=ORIENTED_EDGE ( 'NONE', *, *, #46183, .T. ) ;
#12617=ORIENTED_EDGE ( 'NONE', *, *, #54497, .F. ) ;
#12618=ADVANCED_FACE ( 'NONE', ( #60705 ), #105564, .F. ) ;
#12621=CARTESIAN_POINT ( 'NONE',  ( -21.18398860626899349, 28.73617430169802134, 5.000000000000000000 ) ) ;
#12622=LINE ( 'NONE', #59050, #48515 ) ;
#12624=CARTESIAN_POINT ( 'NONE',  ( -18.48921356237309510, -27.52281430457068367, 5.000000000000000000 ) ) ;
#12625=DIRECTION ( 'NONE',  ( 0.7071067811865487940, 0.7071067811865463515, 0.000000000000000000 ) ) ;
#12626=ADVANCED_FACE ( 'NONE', ( #15673 ), #14292, .F. ) ;
#12627=DIRECTION ( 'NONE',  ( 0.7071067811865487940, 0.7071067811865463515, 0.000000000000000000 ) ) ;
#12628=EDGE_LOOP ( 'NONE', ( #75920, #3059, #132140, #82577 ) ) ;
#12629=ORIENTED_EDGE ( 'NONE', *, *, #141179, .T. ) ;
#12630=LINE ( 'NONE', #80774, #117344 ) ;
#12631=DIRECTION ( 'NONE',  ( 0.3543493200069162685, -0.000000000000000000, -0.9351131265310288487 ) ) ;
#12633=LINE ( 'NONE', #80777, #85252 ) ;
#12634=EDGE_CURVE ( 'NONE', #108829, #13986, #93284, .T. ) ;
#12635=ORIENTED_EDGE ( 'NONE', *, *, #140543, .F. ) ;
#12636=CARTESIAN_POINT ( 'NONE',  ( 0.000000000000000000, 0.000000000000000000, 5.000000000000000000 ) ) ;
#12637=FACE_OUTER_BOUND ( 'NONE', #17083, .T. ) ;
#12639=ORIENTED_EDGE ( 'NONE', *, *, #79343, .T. ) ;
#12640=FACE_OUTER_BOUND ( 'NONE', #48627, .T. ) ;
#12641=DIRECTION ( 'NONE',  ( -0.7071067811865486830, -0.7071067811865464625, -0.000000000000000000 ) ) ;
#12642=UNCERTAINTY_MEASURE_WITH_UNIT (LENGTH_MEASURE( 1.000000000000000082E-05 ), #107224, 'distance_accuracy_value', 'NONE');
#12643=DIRECTION ( 'NONE',  ( -0.7071067811865487940, 0.7071067811865463515, -0.000000000000000000 ) ) ;
#12645=VECTOR ( 'NONE', #57372, 1000.000000000000227 ) ;
#12646=PLANE ( 'NONE',  #58082 ) ;
#12647=EDGE_CURVE ( 'NONE', #134939, #86178, #117158, .T. ) ;
#12648=DIRECTION ( 'NONE',  ( -0.000000000000000000, 0.3543493200069153248, 0.9351131265310292928 ) ) ;
#12649=CARTESIAN_POINT ( 'NONE',  ( -57.29974487139158157, -27.71228299555246011, 4.000000000000000000 ) ) ;
#12650=ORIENTED_EDGE ( 'NONE', *, *, #54130, .F. ) ;
#12651=CARTESIAN_POINT ( 'NONE',  ( -17.67183060077635304, -15.74070752338413115, 4.000000000000000000 ) ) ;
#12652=ORIENTED_EDGE ( 'NONE', *, *, #37822, .T. ) ;
#12653=LINE ( 'NONE', #1742, #82516 ) ;
#12654=DIRECTION ( 'NONE',  ( -0.7071067811865487940, 0.7071067811865463515, 0.000000000000000000 ) ) ;
#12655=FACE_OUTER_BOUND ( 'NONE', #45220, .T. ) ;
#12656=DIRECTION ( 'NONE',  ( -0.7071067811865487940, 0.7071067811865463515, -0.000000000000000000 ) ) ;
#12657=ADVANCED_FACE ( 'NONE', ( #41048 ), #85248, .F. ) ;
#12658=FACE_OUTER_BOUND ( 'NONE', #130438, .T. ) ;
#12660=ORIENTED_EDGE ( 'NONE', *, *, #78037, .F. ) ;
#12661=VERTEX_POINT ( 'NONE', #83875 ) ;
#12662=LINE ( 'NONE', #14084, #37139 ) ;
#12668=DIRECTION ( 'NONE',  ( -0.6830127018922180770, -0.6830127018922204085, -0.2588190451025213501 ) ) ;
#12670=DIRECTION ( 'NONE',  ( -0.7071067811865487940, 0.7071067811865463515, 0.000000000000000000 ) ) ;
#12673=DIRECTION ( 'NONE',  ( 1.000000000000000000, 0.000000000000000000, 0.000000000000000000 ) ) ;
#12674=VECTOR ( 'NONE', #143024, 999.9999999999998863 ) ;
#12675=CARTESIAN_POINT ( 'NONE',  ( 25.17665910159957221, 5.259292476615669010, 15.86257073897091807 ) ) ;
#12677=ORIENTED_EDGE ( 'NONE', *, *, #23334, .F. ) ;
#12678=DIRECTION ( 'NONE',  ( -0.7071067811865486830, -0.7071067811865464625, 0.000000000000000000 ) ) ;
#12680=CARTESIAN_POINT ( 'NONE',  ( 4.499999999999983125, 4.087461875839196956, 4.000000000000000000 ) ) ;
#12682=ORIENTED_EDGE ( 'NONE', *, *, #36771, .F. ) ;
#12684=ORIENTED_EDGE ( 'NONE', *, *, #24389, .T. ) ;
#12686=PLANE ( 'NONE',  #129941 ) ;
#12687=CARTESIAN_POINT ( 'NONE',  ( 27.18398860626900060, 28.73617430169806042, 5.000000000000000000 ) ) ;
#12688=ADVANCED_FACE ( 'NONE', ( #7684 ), #75137, .F. ) ;
#12689=FACE_OUTER_BOUND ( 'NONE', #107718, .T. ) ;
#12690=ORIENTED_EDGE ( 'NONE', *, *, #39874, .T. ) ;
#12691=FACE_OUTER_BOUND ( 'NONE', #89945, .T. ) ;
#12694=LINE ( 'NONE', #137364, #32252 ) ;
#12696=VECTOR ( 'NONE', #131630, 1000.000000000000000 ) ;
#12698=VERTEX_POINT ( 'NONE', #96123 ) ;
#12699=EDGE_CURVE ( 'NONE', #130956, #70680, #30905, .T. ) ;
#12701=AXIS2_PLACEMENT_3D ( 'NONE', #66145, #10987, #99 ) ;
#12702=AXIS2_PLACEMENT_3D ( 'NONE', #107369, #129121, #74039 ) ;
#12703=VERTEX_POINT ( 'NONE', #30159 ) ;
#12705=VECTOR ( 'NONE', #125990, 1000.000000000000000 ) ;
#12707=CARTESIAN_POINT ( 'NONE',  ( 34.92499999999998295, -20.14387692260739016, 4.000000000000000000 ) ) ;
#12708=DIRECTION ( 'NONE',  ( 0.000000000000000000, -1.000000000000000000, 0.000000000000000000 ) ) ;
#12709=EDGE_CURVE ( 'NONE', #129026, #131707, #95419, .T. ) ;
#12710=CARTESIAN_POINT ( 'NONE',  ( -29.99999999999979750, -6.108550654416986525, -3.114665004255035452 ) ) ;
#12713=ORIENTED_EDGE ( 'NONE', *, *, #92159, .T. ) ;
#12714=EDGE_CURVE ( 'NONE', #136079, #127597, #64962, .T. ) ;
#12715=DIRECTION ( 'NONE',  ( 0.7071067811865487940, 0.7071067811865463515, 0.000000000000000000 ) ) ;
#12717=EDGE_CURVE ( 'NONE', #110945, #28039, #141060, .T. ) ;
#12720=DIRECTION ( 'NONE',  ( -0.7071067811865486830, -0.7071067811865464625, 0.000000000000000000 ) ) ;
#12721=CARTESIAN_POINT ( 'NONE',  ( 20.29289321881331531, -6.740707523384211086, 5.000000000000000000 ) ) ;
#12722=VERTEX_POINT ( 'NONE', #107716 ) ;
#12723=EDGE_CURVE ( 'NONE', #489, #35500, #8374, .T. ) ;
#12724=FACE_BOUND ( 'NONE', #5015, .T. ) ;
#12725=DIRECTION ( 'NONE',  ( 0.6830127018922180770, -0.6830127018922204085, -0.2588190451025213501 ) ) ;
#12728=ADVANCED_FACE ( 'NONE', ( #41765 ), #106265, .F. ) ;
#12729=CARTESIAN_POINT ( 'NONE',  ( 32.99451991528749062, 28.92564299267960948, 4.000000000000000000 ) ) ;
#12731=ORIENTED_EDGE ( 'NONE', *, *, #123005, .T. ) ;
#12732=ORIENTED_EDGE ( 'NONE', *, *, #99913, .T. ) ;
#12734=ORIENTED_EDGE ( 'NONE', *, *, #64284, .T. ) ;
#12735=CARTESIAN_POINT ( 'NONE',  ( -30.18398860626900060, 28.73617430169808173, 5.000000000000000000 ) ) ;
#12736=ORIENTED_EDGE ( 'NONE', *, *, #86410, .F. ) ;
#12738=CARTESIAN_POINT ( 'NONE',  ( -27.48921356237309155, -27.52281430457074762, 5.000000000000000000 ) ) ;
#12739=LINE ( 'NONE', #1826, #88801 ) ;
#12740=EDGE_LOOP ( 'NONE', ( #67069, #104615, #85489, #58976 ) ) ;
#12741=DIRECTION ( 'NONE',  ( -0.7071067811865486830, -0.7071067811865464625, 0.000000000000000000 ) ) ;
#12743=CARTESIAN_POINT ( 'NONE',  ( -17.51078643762690845, -27.52281430457043143, 5.000000000000000000 ) ) ;
#12745=FACE_OUTER_BOUND ( 'NONE', #15451, .T. ) ;
#12746=EDGE_CURVE ( 'NONE', #56310, #52592, #75830, .T. ) ;
#12747=PLANE ( 'NONE',  #60100 ) ;
#12748=CARTESIAN_POINT ( 'NONE',  ( 33.18398860626899705, 28.73617430169810305, 5.000000000000000000 ) ) ;
#12751=EDGE_CURVE ( 'NONE', #26635, #44135, #94688, .T. ) ;
#12752=DIRECTION ( 'NONE',  ( 0.7071067811865487940, 0.7071067811865463515, 0.000000000000000000 ) ) ;
#12755=VERTEX_POINT ( 'NONE', #117854 ) ;
#12757=ORIENTED_EDGE ( 'NONE', *, *, #103142, .F. ) ;
#12758=EDGE_CURVE ( 'NONE', #18442, #59390, #18541, .T. ) ;
#12759=DIRECTION ( 'NONE',  ( -0.7071067811865486830, -0.7071067811865464625, 0.000000000000000000 ) ) ;
#12760=VECTOR ( 'NONE', #119467, 999.9999999999998863 ) ;
#12763=CARTESIAN_POINT ( 'NONE',  ( -31.03340032343004040, 6.759292476615653023, 12.28218704918514881 ) ) ;
#12765=VECTOR ( 'NONE', #98451, 999.9999999999998863 ) ;
#12767=ORIENTED_EDGE ( 'NONE', *, *, #117103, .T. ) ;
#12768=CARTESIAN_POINT ( 'NONE',  ( -15.18398860626900237, 28.73617430169797871, 5.000000000000000000 ) ) ;
#12769=CARTESIAN_POINT ( 'NONE',  ( 4.828169399223493308, 12.75929247661559351, 4.000000000000000000 ) ) ;
#12770=EDGE_LOOP ( 'NONE', ( #133551, #5253, #91523, #3136 ) ) ;
#12773=LINE ( 'NONE', #57050, #24311 ) ;
#12774=ORIENTED_EDGE ( 'NONE', *, *, #128213, .T. ) ;
#12775=CARTESIAN_POINT ( 'NONE',  ( -41.39513766812454776, 21.75929247661549226, 21.32995629748196009 ) ) ;
#12776=VECTOR ( 'NONE', #53693, 1000.000000000000000 ) ;
#12777=ORIENTED_EDGE ( 'NONE', *, *, #89514, .T. ) ;
#12778=ORIENTED_EDGE ( 'NONE', *, *, #109795, .T. ) ;
#12779=VERTEX_POINT ( 'NONE', #39650 ) ;
#12782=LINE ( 'NONE', #4007, #102656 ) ;
#12783=ADVANCED_FACE ( 'NONE', ( #37128 ), #33074, .F. ) ;
#12784=CARTESIAN_POINT ( 'NONE',  ( 25.35824297541124750, 15.75929247661555799, 19.34181609438693528 ) ) ;
#12786=CARTESIAN_POINT ( 'NONE',  ( -19.59167451900987089, -0.7407075233842665973, 14.76736230305375841 ) ) ;
#12787=ORIENTED_EDGE ( 'NONE', *, *, #45365, .T. ) ;
#12789=VECTOR ( 'NONE', #84732, 1000.000000000000000 ) ;
#12790=VECTOR ( 'NONE', #90916, 1000.000000000000000 ) ;
#12794=CARTESIAN_POINT ( 'NONE',  ( -27.70701326429286127, -21.74070752338406365, 4.999753212805221558 ) ) ;
#12795=EDGE_CURVE ( 'NONE', #8995, #116753, #143214, .T. ) ;
#12797=LINE ( 'NONE', #124429, #65264 ) ;
#12798=ORIENTED_EDGE ( 'NONE', *, *, #28759, .T. ) ;
#12799=ORIENTED_EDGE ( 'NONE', *, *, #1838, .F. ) ;
#12800=ORIENTED_EDGE ( 'NONE', *, *, #95656, .F. ) ;
#12802=CARTESIAN_POINT ( 'NONE',  ( -34.92500000000001137, -18.18334561358938473, 4.500000000000000888 ) ) ;
#12804=PLANE ( 'NONE',  #128302 ) ;
#12805=FACE_OUTER_BOUND ( 'NONE', #12032, .T. ) ;
#12806=EDGE_CURVE ( 'NONE', #32218, #22939, #65707, .T. ) ;
#12808=ADVANCED_FACE ( 'NONE', ( #110556 ), #142520, .F. ) ;
#12809=LINE ( 'NONE', #79571, #50711 ) ;
#12810=EDGE_CURVE ( 'NONE', #54347, #111783, #26266, .T. ) ;
#12811=CARTESIAN_POINT ( 'NONE',  ( 32.99451991528749062, 28.92564299267960948, 4.000000000000000000 ) ) ;
#12812=CARTESIAN_POINT ( 'NONE',  ( 41.99451991528749062, 28.92564299267967343, 4.000000000000000000 ) ) ;
#12813=CARTESIAN_POINT ( 'NONE',  ( -54.48921356237310221, -27.52281430457093236, 5.000000000000000000 ) ) ;
#12814=FACE_OUTER_BOUND ( 'NONE', #138041, .T. ) ;
#12815=ORIENTED_EDGE ( 'NONE', *, *, #115188, .T. ) ;
#12816=ORIENTED_EDGE ( 'NONE', *, *, #43085, .T. ) ;
#12817=DIRECTION ( 'NONE',  ( -0.7071067811865486830, -0.7071067811865464625, 0.000000000000000000 ) ) ;
#12818=CARTESIAN_POINT ( 'NONE',  ( -34.42500000000001137, 14.97718569542927014, 5.000000000000000000 ) ) ;
#12820=EDGE_CURVE ( 'NONE', #39673, #116876, #109871, .T. ) ;
#12822=CARTESIAN_POINT ( 'NONE',  ( -15.18398860626900237, 28.73617430169797871, 5.000000000000000000 ) ) ;
#12823=ORIENTED_EDGE ( 'NONE', *, *, #36228, .T. ) ;
#12824=EDGE_LOOP ( 'NONE', ( #52031, #20705, #9922, #6358, #36111 ) ) ;
#12825=CARTESIAN_POINT ( 'NONE',  ( 34.92499999999998295, 22.22500000000000142, 0.4999999999999995559 ) ) ;
#12826=ORIENTED_EDGE ( 'NONE', *, *, #61486, .F. ) ;
#12827=CARTESIAN_POINT ( 'NONE',  ( -2.292893218813438772, 2.259292476615690770, 5.000000000000000000 ) ) ;
#12829=LINE ( 'NONE', #101285, #127350 ) ;
#12830=LINE ( 'NONE', #80280, #45959 ) ;
#12831=ORIENTED_EDGE ( 'NONE', *, *, #105191, .F. ) ;
#12834=CARTESIAN_POINT ( 'NONE',  ( 15.48921356237309510, -27.52281430457066236, 5.000000000000000000 ) ) ;
#12837=CARTESIAN_POINT ( 'NONE',  ( 14.70025512860841133, -27.71228299555195917, 4.000000000000000000 ) ) ;
#12838=DIRECTION ( 'NONE',  ( -0.7071067811865487940, 0.7071067811865463515, -0.000000000000000000 ) ) ;
#12839=ORIENTED_EDGE ( 'NONE', *, *, #42869, .F. ) ;
#12840=ORIENTED_EDGE ( 'NONE', *, *, #13550, .F. ) ;
#12841=LINE ( 'NONE', #46241, #16700 ) ;
#12842=ORIENTED_EDGE ( 'NONE', *, *, #27836, .T. ) ;
#12844=PLANE ( 'NONE',  #126671 ) ;
#12845=CARTESIAN_POINT ( 'NONE',  ( 7.930039745135869289, -0.7407075233842770334, 13.87443053587609398 ) ) ;
#12846=ADVANCED_FACE ( 'NONE', ( #32325 ), #44665, .F. ) ;
#12847=CARTESIAN_POINT ( 'NONE',  ( 12.48921356237309155, -27.52281430457064104, 5.000000000000000000 ) ) ;
#12851=DIRECTION ( 'NONE',  ( 0.7071067811865487940, 0.7071067811865463515, 0.000000000000000000 ) ) ;
#12852=DIRECTION ( 'NONE',  ( 0.7071067811865487940, 0.7071067811865463515, 0.000000000000000000 ) ) ;
#12853=ORIENTED_EDGE ( 'NONE', *, *, #13618, .T. ) ;
#12854=DIRECTION ( 'NONE',  ( -0.6830127018922181881, 0.6830127018922202975, -0.2588190451025214056 ) ) ;
#12856=DIRECTION ( 'NONE',  ( -0.6830127018922180770, -0.6830127018922204085, -0.2588190451025213501 ) ) ;
#12857=EDGE_LOOP ( 'NONE', ( #60370, #5641, #119389 ) ) ;
#12858=DIRECTION ( 'NONE',  ( 0.7071067811865487940, 0.7071067811865463515, -0.000000000000000000 ) ) ;
#12859=DIRECTION ( 'NONE',  ( 1.000000000000000000, 0.000000000000000000, 0.000000000000000000 ) ) ;
#12860=PLANE ( 'NONE',  #24824 ) ;
#12861=CARTESIAN_POINT ( 'NONE',  ( 34.42499999999998295, -7.458600742197882383, 5.000000000000000000 ) ) ;
#12862=ORIENTED_EDGE ( 'NONE', *, *, #122342, .T. ) ;
#12864=VERTEX_POINT ( 'NONE', #54798 ) ;
#12865=ORIENTED_EDGE ( 'NONE', *, *, #1610, .F. ) ;
#12866=EDGE_CURVE ( 'NONE', #53228, #8502, #98977, .T. ) ;
#12869=ORIENTED_EDGE ( 'NONE', *, *, #56631, .F. ) ;
#12870=EDGE_CURVE ( 'NONE', #86631, #69033, #111279, .T. ) ;
#12871=EDGE_CURVE ( 'NONE', #120303, #117585, #25528, .T. ) ;
#12872=VECTOR ( 'NONE', #64986, 999.9999999999998863 ) ;
#12873=CARTESIAN_POINT ( 'NONE',  ( 14.67183060077637968, -3.740707523384234623, 4.000000000000000000 ) ) ;
#12874=CARTESIAN_POINT ( 'NONE',  ( -34.75611968250420603, 10.70565069852396434, 4.955485411084901592 ) ) ;
#12875=EDGE_CURVE ( 'NONE', #84298, #41034, #77973, .T. ) ;
#12876=PLANE ( 'NONE',  #117407 ) ;
#12878=ORIENTED_EDGE ( 'NONE', *, *, #44624, .T. ) ;
#12879=EDGE_CURVE ( 'NONE', #101519, #117394, #91526, .T. ) ;
#12880=CARTESIAN_POINT ( 'NONE',  ( 33.29974487139158867, -27.71228299555229313, 4.000000000000000000 ) ) ;
#12881=LINE ( 'NONE', #58609, #85947 ) ;
#12882=LINE ( 'NONE', #112231, #83484 ) ;
#12885=VERTEX_POINT ( 'NONE', #113977 ) ;
#12886=EDGE_CURVE ( 'NONE', #71177, #23274, #58950, .T. ) ;
#12887=DIRECTION ( 'NONE',  ( -0.7071067811865487940, 0.7071067811865463515, -0.000000000000000000 ) ) ;
#12888=CARTESIAN_POINT ( 'NONE',  ( -32.20710678118632586, 3.759292476615683665, 5.000000000000000000 ) ) ;
#12889=VERTEX_POINT ( 'NONE', #84918 ) ;
#12891=EDGE_CURVE ( 'NONE', #96290, #138539, #18192, .T. ) ;
#12892=CARTESIAN_POINT ( 'NONE',  ( 34.42499999999998295, 17.97718569542920619, 5.000000000000000000 ) ) ;
#12893=EDGE_CURVE ( 'NONE', #28113, #15358, #37872, .T. ) ;
#12894=CARTESIAN_POINT ( 'NONE',  ( 15.18398860626900237, 28.73617430169797871, 5.000000000000000000 ) ) ;
#12895=DIRECTION ( 'NONE',  ( -0.000000000000000000, -0.3543493200069152693, 0.9351131265310292928 ) ) ;
#12896=EDGE_CURVE ( 'NONE', #97018, #92519, #103785, .T. ) ;
#12897=VECTOR ( 'NONE', #8386, 999.9999999999998863 ) ;
#12898=FACE_OUTER_BOUND ( 'NONE', #117350, .T. ) ;
#12899=PLANE ( 'NONE',  #68232 ) ;
#12900=VECTOR ( 'NONE', #127163, 1000.000000000000000 ) ;
#12902=VECTOR ( 'NONE', #90135, 999.9999999999998863 ) ;
#12903=ORIENTED_EDGE ( 'NONE', *, *, #75289, .F. ) ;
#12904=PLANE ( 'NONE',  #122065 ) ;
#12910=EDGE_LOOP ( 'NONE', ( #6892, #25467, #78587 ) ) ;
#12911=DIRECTION ( 'NONE',  ( 0.7071067811865486830, -0.7071067811865464625, -0.000000000000000000 ) ) ;
#12913=CYLINDRICAL_SURFACE ( 'NONE', #13256, 0.5000000000000004441 ) ;
#12914=ADVANCED_FACE ( 'NONE', ( #116831 ), #114674, .F. ) ;
#12915=DIRECTION ( 'NONE',  ( -0.000000000000000000, 0.000000000000000000, 1.000000000000000000 ) ) ;
#12916=DIRECTION ( 'NONE',  ( -0.3543493200069162685, -0.000000000000000000, -0.9351131265310288487 ) ) ;
#12918=LINE ( 'NONE', #45603, #127425 ) ;
#12919=EDGE_LOOP ( 'NONE', ( #90702, #37490, #129900, #95507 ) ) ;
#12920=DIRECTION ( 'NONE',  ( 0.6830127018922181881, 0.6830127018922202975, -0.2588190451025214056 ) ) ;
#12921=ORIENTED_EDGE ( 'NONE', *, *, #46847, .T. ) ;
#12923=ORIENTED_EDGE ( 'NONE', *, *, #14943, .T. ) ;
#12924=DIRECTION ( 'NONE',  ( 0.7071067811865486830, -0.7071067811865464625, -0.000000000000000000 ) ) ;
#12925=ORIENTED_EDGE ( 'NONE', *, *, #126330, .T. ) ;
#12926=EDGE_CURVE ( 'NONE', #113088, #55705, #82796, .T. ) ;
#12927=ORIENTED_EDGE ( 'NONE', *, *, #72659, .T. ) ;
#12928=ORIENTED_EDGE ( 'NONE', *, *, #72173, .T. ) ;
#12929=ADVANCED_FACE ( 'NONE', ( #94358 ), #138598, .T. ) ;
#12932=CARTESIAN_POINT ( 'NONE',  ( 25.17183060077629975, 0.7592924766157207461, 4.000000000000000000 ) ) ;
#12934=DIRECTION ( 'NONE',  ( 0.6830127018922181881, 0.6830127018922202975, -0.2588190451025214056 ) ) ;
#12935=EDGE_CURVE ( 'NONE', #18415, #100098, #73351, .T. ) ;
#12936=CARTESIAN_POINT ( 'NONE',  ( -28.80981832425534606, -18.74070752338408852, 7.910009926591575535 ) ) ;
#12937=PLANE ( 'NONE',  #65236 ) ;
#12938=DIRECTION ( 'NONE',  ( 1.000000000000000000, 0.000000000000000000, 0.000000000000000000 ) ) ;
#12939=LINE ( 'NONE', #33334, #13523 ) ;
#12940=EDGE_LOOP ( 'NONE', ( #59977, #108801, #34420, #38257 ) ) ;
#12941=DIRECTION ( 'NONE',  ( -0.6830127018922181881, 0.6830127018922202975, -0.2588190451025214056 ) ) ;
#12942=CARTESIAN_POINT ( 'NONE',  ( -63.29974487139158867, -27.71228299555250274, 4.000000000000000000 ) ) ;
#12943=PLANE ( 'NONE',  #65703 ) ;
#12944=ADVANCED_FACE ( 'NONE', ( #137170 ), #28408, .F. ) ;
#12946=ORIENTED_EDGE ( 'NONE', *, *, #143524, .F. ) ;
#12948=ORIENTED_EDGE ( 'NONE', *, *, #142978, .T. ) ;
#12949=LINE ( 'NONE', #1353, #14361 ) ;
#12951=CARTESIAN_POINT ( 'NONE',  ( -26.99451991528749417, 28.92564299267956685, 4.000000000000000000 ) ) ;
#12952=EDGE_CURVE ( 'NONE', #138262, #6023, #104522, .T. ) ;
#12953=CARTESIAN_POINT ( 'NONE',  ( -11.99999999999992006, -1.068876922607800761, 4.000000000000000000 ) ) ;
#12954=CARTESIAN_POINT ( 'NONE',  ( -14.18753812416042770, -22.22500000000000142, 4.000000000000000000 ) ) ;
#12955=EDGE_CURVE ( 'NONE', #121709, #68092, #60339, .T. ) ;
#12956=ORIENTED_EDGE ( 'NONE', *, *, #84508, .F. ) ;
#12957=PLANE ( 'NONE',  #51051 ) ;
#12958=ORIENTED_EDGE ( 'NONE', *, *, #81534, .F. ) ;
#12959=CARTESIAN_POINT ( 'NONE',  ( -14.99999999999989519, -21.84840872380826227, 2.849755605029573591 ) ) ;
#12960=VECTOR ( 'NONE', #128311, 1000.000000000000000 ) ;
#12962=EDGE_LOOP ( 'NONE', ( #128129, #75582, #104105, #15694 ) ) ;
#12965=VECTOR ( 'NONE', #94903, 1000.000000000000000 ) ;
#12966=FACE_OUTER_BOUND ( 'NONE', #54057, .T. ) ;
#12967=EDGE_CURVE ( 'NONE', #31893, #57582, #5179, .T. ) ;
#12968=ORIENTED_EDGE ( 'NONE', *, *, #31406, .F. ) ;
#12969=VERTEX_POINT ( 'NONE', #49476 ) ;
#12970=ORIENTED_EDGE ( 'NONE', *, *, #112715, .T. ) ;
#12971=CARTESIAN_POINT ( 'NONE',  ( -8.700255128608413102, -27.71228299555199825, 4.000000000000000000 ) ) ;
#12972=CARTESIAN_POINT ( 'NONE',  ( -65.99451991528749772, 28.92564299267984396, 4.000000000000000000 ) ) ;
#12973=DIRECTION ( 'NONE',  ( 0.7071067811865487940, -0.7071067811865463515, 0.000000000000000000 ) ) ;
#12974=PLANE ( 'NONE',  #121342 ) ;
#12975=ORIENTED_EDGE ( 'NONE', *, *, #74363, .T. ) ;
#12976=EDGE_CURVE ( 'NONE', #68408, #93537, #93666, .T. ) ;
#12977=AXIS2_PLACEMENT_3D ( 'NONE', #112007, #56925, #80108 ) ;
#12980=ORIENTED_EDGE ( 'NONE', *, *, #11098, .F. ) ;
#12981=LINE ( 'NONE', #47124, #53982 ) ;
#12982=VERTEX_POINT ( 'NONE', #38564 ) ;
#12983=EDGE_CURVE ( 'NONE', #21557, #8470, #7331, .T. ) ;
#12985=ORIENTED_EDGE ( 'NONE', *, *, #10702, .F. ) ;
#12986=VECTOR ( 'NONE', #96143, 1000.000000000000000 ) ;
#12987=VERTEX_POINT ( 'NONE', #116107 ) ;
#12989=CARTESIAN_POINT ( 'NONE',  ( 60.29974487139158867, -27.71228299555248142, 4.000000000000000000 ) ) ;
#12990=CARTESIAN_POINT ( 'NONE',  ( 7.499999999999952927, 0.4311230773921831960, 4.000000000000000000 ) ) ;
#12991=VERTEX_POINT ( 'NONE', #16804 ) ;
#12992=DIRECTION ( 'NONE',  ( -0.7071067811865486830, -0.7071067811865464625, 0.000000000000000000 ) ) ;
#12994=ORIENTED_EDGE ( 'NONE', *, *, #24543, .T. ) ;
#12996=AXIS2_PLACEMENT_3D ( 'NONE', #140908, #72871, #85820 ) ;
#12997=LINE ( 'NONE', #101447, #36003 ) ;
#12999=AXIS2_PLACEMENT_3D ( 'NONE', #28918, #4975, #28210 ) ;
#13000=CARTESIAN_POINT ( 'NONE',  ( -20.99999999999985079, -15.41253812416059787, 4.000000000000000000 ) ) ;
#13002=FACE_OUTER_BOUND ( 'NONE', #32844, .T. ) ;
#13003=AXIS2_PLACEMENT_3D ( 'NONE', #138407, #15858, #49984 ) ;
#13004=DIRECTION ( 'NONE',  ( 0.000000000000000000, -1.000000000000000000, 0.000000000000000000 ) ) ;
#13006=CARTESIAN_POINT ( 'NONE',  ( 57.48921356237308800, -27.52281430457095368, 5.000000000000000000 ) ) ;
#13008=DIRECTION ( 'NONE',  ( 0.7071067811865487940, 0.7071067811865463515, -0.000000000000000000 ) ) ;
#13010=VECTOR ( 'NONE', #125371, 1000.000000000000227 ) ;
#13011=CARTESIAN_POINT ( 'NONE',  ( -0.4892135623730947680, -27.52281430457055578, 5.000000000000000000 ) ) ;
#13013=ORIENTED_EDGE ( 'NONE', *, *, #109605, .T. ) ;
#13014=EDGE_CURVE ( 'NONE', #57955, #99416, #61083, .T. ) ;
#13017=ORIENTED_EDGE ( 'NONE', *, *, #58467, .T. ) ;
#13019=VERTEX_POINT ( 'NONE', #127728 ) ;
#13020=DIRECTION ( 'NONE',  ( 0.7071067811865486830, -0.7071067811865464625, -0.000000000000000000 ) ) ;
#13021=CARTESIAN_POINT ( 'NONE',  ( 42.18398860626899705, 28.73617430169816700, 5.000000000000000000 ) ) ;
#13022=DIRECTION ( 'NONE',  ( 1.000000000000000000, 0.000000000000000000, 0.000000000000000000 ) ) ;
#13023=EDGE_LOOP ( 'NONE', ( #4793, #26703, #60983, #43694 ) ) ;
#13025=CARTESIAN_POINT ( 'NONE',  ( 7.499999999999948486, -16.91253812416058011, 4.000000000000000000 ) ) ;
#13026=FACE_OUTER_BOUND ( 'NONE', #111403, .T. ) ;
#13028=VERTEX_POINT ( 'NONE', #55158 ) ;
#13029=CARTESIAN_POINT ( 'NONE',  ( -14.51078643762690490, -27.52281430457045275, 5.000000000000000000 ) ) ;
#13030=CARTESIAN_POINT ( 'NONE',  ( -25.49999999999981881, 3.431123077392149501, 4.000000000000000000 ) ) ;
#13031=ADVANCED_FACE ( 'NONE', ( #76194 ), #9461, .T. ) ;
#13033=DIRECTION ( 'NONE',  ( 0.7071067811865487940, 0.7071067811865463515, 0.000000000000000000 ) ) ;
#13034=LINE ( 'NONE', #90638, #96294 ) ;
#13035=LINE ( 'NONE', #44287, #36020 ) ;
#13037=EDGE_CURVE ( 'NONE', #119486, #81792, #74047, .T. ) ;
#13042=VERTEX_POINT ( 'NONE', #132743 ) ;
#13043=EDGE_CURVE ( 'NONE', #92202, #114427, #43555, .T. ) ;
#13044=LINE ( 'NONE', #47188, #77965 ) ;
#13045=AXIS2_PLACEMENT_3D ( 'NONE', #51941, #129472, #62827 ) ;
#13046=LINE ( 'NONE', #14495, #124468 ) ;
#13047=EDGE_CURVE ( 'NONE', #26531, #118332, #42153, .T. ) ;
#13048=EDGE_CURVE ( 'NONE', #75885, #13822, #64596, .T. ) ;
#13049=CARTESIAN_POINT ( 'NONE',  ( -11.81601139373100651, 28.73617430169779041, 5.000000000000000000 ) ) ;
#13052=EDGE_LOOP ( 'NONE', ( #26514, #60550, #59326, #131306 ) ) ;
#13053=ORIENTED_EDGE ( 'NONE', *, *, #80612, .T. ) ;
#13054=VECTOR ( 'NONE', #33036, 999.9999999999998863 ) ;
#13055=CARTESIAN_POINT ( 'NONE',  ( -24.48921356237309510, -27.52281430457072631, 5.000000000000000000 ) ) ;
#13057=VERTEX_POINT ( 'NONE', #119653 ) ;
#13058=EDGE_CURVE ( 'NONE', #143372, #99698, #97940, .T. ) ;
#13059=ORIENTED_EDGE ( 'NONE', *, *, #44627, .T. ) ;
#13060=CARTESIAN_POINT ( 'NONE',  ( 0.000000000000000000, 0.000000000000000000, 5.000000000000000000 ) ) ;
#13063=EDGE_CURVE ( 'NONE', #140203, #78331, #97176, .T. ) ;
#13064=VECTOR ( 'NONE', #142412, 1000.000000000000000 ) ;
#13065=DIRECTION ( 'NONE',  ( 0.7071067811865486830, -0.7071067811865464625, -0.000000000000000000 ) ) ;
#13066=ORIENTED_EDGE ( 'NONE', *, *, #28168, .T. ) ;
#13067=AXIS2_PLACEMENT_3D ( 'NONE', #75870, #120032, #51978 ) ;
#13069=LINE ( 'NONE', #114536, #131191 ) ;
#13070=ORIENTED_EDGE ( 'NONE', *, *, #91129, .F. ) ;
#13071=ORIENTED_EDGE ( 'NONE', *, *, #19603, .F. ) ;
#13073=VERTEX_POINT ( 'NONE', #65343 ) ;
#13077=ORIENTED_EDGE ( 'NONE', *, *, #123429, .T. ) ;
#13078=DIRECTION ( 'NONE',  ( -0.000000000000000000, 0.000000000000000000, 1.000000000000000000 ) ) ;
#13079=LINE ( 'NONE', #47907, #126577 ) ;
#13080=ADVANCED_FACE ( 'NONE', ( #87064 ), #63897, .F. ) ;
#13082=FACE_BOUND ( 'NONE', #36726, .T. ) ;
#13085=CARTESIAN_POINT ( 'NONE',  ( 0.000000000000000000, 0.000000000000000000, 5.000000000000000000 ) ) ;
#13086=FACE_OUTER_BOUND ( 'NONE', #140068, .T. ) ;
#13087=DIRECTION ( 'NONE',  ( -0.6830127018922181881, 0.6830127018922202975, -0.2588190451025214056 ) ) ;
#13088=ORIENTED_EDGE ( 'NONE', *, *, #96736, .F. ) ;
#13089=EDGE_CURVE ( 'NONE', #19080, #112760, #31967, .T. ) ;
#13090=CARTESIAN_POINT ( 'NONE',  ( -3.299744871391591339, -27.71228299555208352, 4.000000000000000000 ) ) ;
#13091=ORIENTED_EDGE ( 'NONE', *, *, #120157, .T. ) ;
#13092=EDGE_CURVE ( 'NONE', #74639, #46818, #10891, .T. ) ;
#13093=ORIENTED_EDGE ( 'NONE', *, *, #34640, .T. ) ;
#13095=VERTEX_POINT ( 'NONE', #99336 ) ;
#13098=AXIS2_PLACEMENT_3D ( 'NONE', #86873, #85410, #65139 ) ;
#13100=VERTEX_POINT ( 'NONE', #132008 ) ;
#13101=VECTOR ( 'NONE', #103383, 1000.000000000000227 ) ;
#13102=FACE_OUTER_BOUND ( 'NONE', #16725, .T. ) ;
#13103=DIRECTION ( 'NONE',  ( 0.3543493200069162685, -0.000000000000000000, -0.9351131265310288487 ) ) ;
#13104=EDGE_LOOP ( 'NONE', ( #126659, #13650, #10805, #107861, #22527 ) ) ;
#13105=CARTESIAN_POINT ( 'NONE',  ( 34.92499999999998295, -4.298069433178973497, 4.500000000000000888 ) ) ;
#13106=LINE ( 'NONE', #13808, #57468 ) ;
#13107=AXIS2_PLACEMENT_3D ( 'NONE', #29598, #73836, #118010 ) ;
#13108=CARTESIAN_POINT ( 'NONE',  ( 57.48921356237308800, -27.52281430457095368, 5.000000000000000000 ) ) ;
#13109=DIRECTION ( 'NONE',  ( -0.000000000000000000, 0.3543493200069153248, 0.9351131265310292928 ) ) ;
#13113=ORIENTED_EDGE ( 'NONE', *, *, #104923, .T. ) ;
#13114=ORIENTED_EDGE ( 'NONE', *, *, #90415, .F. ) ;
#13116=CARTESIAN_POINT ( 'NONE',  ( -13.49999999999990408, -11.56887692260769995, 4.000000000000000000 ) ) ;
#13117=VERTEX_POINT ( 'NONE', #44295 ) ;
#13120=DIRECTION ( 'NONE',  ( 0.7071067811865486830, -0.7071067811865464625, -0.000000000000000000 ) ) ;
#13121=ORIENTED_EDGE ( 'NONE', *, *, #126924, .T. ) ;
#13123=LINE ( 'NONE', #90737, #56066 ) ;
#13125=AXIS2_PLACEMENT_3D ( 'NONE', #46365, #123899, #24556 ) ;
#13126=LINE ( 'NONE', #1527, #29891 ) ;
#13127=ORIENTED_EDGE ( 'NONE', *, *, #48184, .T. ) ;
#13129=DIRECTION ( 'NONE',  ( 0.7071067811865487940, 0.7071067811865463515, -0.000000000000000000 ) ) ;
#13130=CARTESIAN_POINT ( 'NONE',  ( 26.99999999999981881, 14.96639925780211122, 5.000000000000000000 ) ) ;
#13131=CARTESIAN_POINT ( 'NONE',  ( 12.51665438641036054, 22.22500000000000142, 4.500000000000000888 ) ) ;
#13132=ORIENTED_EDGE ( 'NONE', *, *, #116955, .T. ) ;
#13133=DIRECTION ( 'NONE',  ( -0.000000000000000000, -0.000000000000000000, 1.000000000000000000 ) ) ;
#13134=LINE ( 'NONE', #834, #28650 ) ;
#13135=ORIENTED_EDGE ( 'NONE', *, *, #23899, .F. ) ;
#13136=VECTOR ( 'NONE', #5893, 1000.000000000000000 ) ;
#13137=CARTESIAN_POINT ( 'NONE',  ( 2.843876922607555091, -22.22500000000000497, 4.000000000000000000 ) ) ;
#13138=VERTEX_POINT ( 'NONE', #66052 ) ;
#13139=FACE_OUTER_BOUND ( 'NONE', #26170, .T. ) ;
#13141=CARTESIAN_POINT ( 'NONE',  ( -26.99999999999981171, -3.485240976185098649, -4.108735105802460374 ) ) ;
#13143=VERTEX_POINT ( 'NONE', #129851 ) ;
#13144=DIRECTION ( 'NONE',  ( 1.000000000000000000, 0.000000000000000000, 0.000000000000000000 ) ) ;
#13145=DIRECTION ( 'NONE',  ( -0.7071067811865487940, 0.7071067811865463515, -0.000000000000000000 ) ) ;
#13146=DIRECTION ( 'NONE',  ( -0.6830127018922181881, 0.6830127018922202975, -0.2588190451025214056 ) ) ;
#13147=AXIS2_PLACEMENT_3D ( 'NONE', #64735, #20489, #76333 ) ;
#13149=CARTESIAN_POINT ( 'NONE',  ( -7.499999999999944045, -7.420205493532908037, -2.617629953481270366 ) ) ;
#13150=VERTEX_POINT ( 'NONE', #41404 ) ;
#13152=EDGE_CURVE ( 'NONE', #33921, #127932, #30552, .T. ) ;
#13153=LINE ( 'NONE', #101609, #136645 ) ;
#13154=VERTEX_POINT ( 'NONE', #74787 ) ;
#13155=EDGE_CURVE ( 'NONE', #56699, #116635, #19658, .T. ) ;
#13156=VERTEX_POINT ( 'NONE', #100795 ) ;
#13158=LINE ( 'NONE', #111036, #13505 ) ;
#13159=ORIENTED_EDGE ( 'NONE', *, *, #87063, .T. ) ;
#13160=DIRECTION ( 'NONE',  ( 0.3543493200069162685, -0.000000000000000000, -0.9351131265310288487 ) ) ;
#13161=DIRECTION ( 'NONE',  ( 0.7071067811865487940, 0.7071067811865463515, 0.000000000000000000 ) ) ;
#13162=VECTOR ( 'NONE', #56297, 1000.000000000000000 ) ;
#13164=ADVANCED_FACE ( 'NONE', ( #34839 ), #113079, .F. ) ;
#13165=DIRECTION ( 'NONE',  ( 0.7071067811865487940, -0.7071067811865463515, 0.000000000000000000 ) ) ;
#13166=LINE ( 'NONE', #34244, #35116 ) ;
#13167=CARTESIAN_POINT ( 'NONE',  ( 24.29974487139158867, -27.71228299555223273, 4.000000000000000000 ) ) ;
#13168=DIRECTION ( 'NONE',  ( -0.000000000000000000, -0.3543493200069152693, 0.9351131265310292928 ) ) ;
#13169=PLANE ( 'NONE',  #115431 ) ;
#13170=CARTESIAN_POINT ( 'NONE',  ( 13.49999999999990763, -16.91253812416058722, 4.000000000000000000 ) ) ;
#13171=VERTEX_POINT ( 'NONE', #33435 ) ;
#13172=EDGE_CURVE ( 'NONE', #7538, #34146, #77638, .T. ) ;
#13173=VERTEX_POINT ( 'NONE', #79081 ) ;
#13174=VERTEX_POINT ( 'NONE', #68904 ) ;
#13175=CARTESIAN_POINT ( 'NONE',  ( -32.20710678118631876, -14.24070752338413826, 5.000000000000000000 ) ) ;
#13176=ORIENTED_EDGE ( 'NONE', *, *, #51882, .F. ) ;
#13180=LINE ( 'NONE', #101639, #131934 ) ;
#13181=EDGE_CURVE ( 'NONE', #92161, #82100, #57319, .T. ) ;
#13182=ORIENTED_EDGE ( 'NONE', *, *, #99759, .T. ) ;
#13183=DIRECTION ( 'NONE',  ( 1.000000000000000000, 0.000000000000000000, 0.000000000000000000 ) ) ;
#13184=FACE_OUTER_BOUND ( 'NONE', #108539, .T. ) ;
#13186=VECTOR ( 'NONE', #17361, 1000.000000000000000 ) ;
#13187=LINE ( 'NONE', #33575, #115899 ) ;
#13189=EDGE_LOOP ( 'NONE', ( #97611, #89483, #10773, #70595 ) ) ;
#13190=DIRECTION ( 'NONE',  ( -0.7071067811865486830, 0.7071067811865464625, 0.000000000000000000 ) ) ;
#13194=CARTESIAN_POINT ( 'NONE',  ( -28.49999999999981171, -1.592773361805396970, -6.492772025301164263 ) ) ;
#13195=VECTOR ( 'NONE', #35060, 999.9999999999998863 ) ;
#13196=DIRECTION ( 'NONE',  ( -0.7071067811865486830, -0.7071067811865464625, 0.000000000000000000 ) ) ;
#13197=DIRECTION ( 'NONE',  ( 0.6830127018922180770, -0.6830127018922204085, -0.2588190451025213501 ) ) ;
#13198=AXIS2_PLACEMENT_3D ( 'NONE', #65572, #112604, #110433 ) ;
#13201=LINE ( 'NONE', #79960, #72270 ) ;
#13202=VECTOR ( 'NONE', #116832, 1000.000000000000227 ) ;
#13203=FACE_OUTER_BOUND ( 'NONE', #50608, .T. ) ;
#13205=ORIENTED_EDGE ( 'NONE', *, *, #97654, .F. ) ;
#13207=ORIENTED_EDGE ( 'NONE', *, *, #121695, .F. ) ;
#13209=EDGE_CURVE ( 'NONE', #142320, #71285, #12341, .T. ) ;
#13212=ORIENTED_EDGE ( 'NONE', *, *, #30257, .F. ) ;
#13213=CARTESIAN_POINT ( 'NONE',  ( -18.18398860626898994, 28.73617430169800002, 5.000000000000000000 ) ) ;
#13215=EDGE_CURVE ( 'NONE', #124077, #123774, #10752, .T. ) ;
#13216=ADVANCED_FACE ( 'NONE', ( #11601 ), #92040, .F. ) ;
#13218=EDGE_LOOP ( 'NONE', ( #4820, #80961, #29837, #50615 ) ) ;
#13219=DIRECTION ( 'NONE',  ( 0.7071067811865487940, 0.7071067811865463515, 0.000000000000000000 ) ) ;
#13220=VERTEX_POINT ( 'NONE', #1445 ) ;
#13221=CARTESIAN_POINT ( 'NONE',  ( 28.49999999999979750, -11.56887692260769640, 4.000000000000000000 ) ) ;
#13222=ADVANCED_FACE ( 'NONE', ( #13750 ), #102942, .F. ) ;
#13223=DIRECTION ( 'NONE',  ( 0.6830127018922181881, 0.6830127018922202975, -0.2588190451025214056 ) ) ;
#13224=CARTESIAN_POINT ( 'NONE',  ( -14.59122188827396549, 7.143407583703162089, 5.000000000000000000 ) ) ;
#13225=EDGE_LOOP ( 'NONE', ( #138154, #31002, #126380 ) ) ;
#13227=DIRECTION ( 'NONE',  ( -0.7071067811865486830, -0.7071067811865464625, 0.000000000000000000 ) ) ;
#13228=VERTEX_POINT ( 'NONE', #102240 ) ;
#13229=DIRECTION ( 'NONE',  ( -0.7071067811865487940, 0.7071067811865463515, 0.000000000000000000 ) ) ;
#13230=EDGE_CURVE ( 'NONE', #3922, #115259, #13044, .T. ) ;
#13231=DIRECTION ( 'NONE',  ( -0.7071067811865486830, -0.7071067811865464625, 0.000000000000000000 ) ) ;
#13232=PLANE ( 'NONE',  #107880 ) ;
#13234=PLANE ( 'NONE',  #11608 ) ;
#13235=PLANE ( 'NONE',  #97076 ) ;
#13237=VECTOR ( 'NONE', #14134, 1000.000000000000000 ) ;
#13238=ADVANCED_FACE ( 'NONE', ( #89214 ), #68215, .F. ) ;
#13241=PLANE ( 'NONE',  #46461 ) ;
#13242=DIRECTION ( 'NONE',  ( -0.7071067811865486830, 0.7071067811865464625, 0.000000000000000000 ) ) ;
#13243=CARTESIAN_POINT ( 'NONE',  ( 57.29974487139158157, -27.71228299555246011, 4.000000000000000000 ) ) ;
#13244=ORIENTED_EDGE ( 'NONE', *, *, #100533, .T. ) ;
#13245=ORIENTED_EDGE ( 'NONE', *, *, #62266, .T. ) ;
#13246=VECTOR ( 'NONE', #78168, 999.9999999999998863 ) ;
#13247=DIRECTION ( 'NONE',  ( 0.000000000000000000, 1.000000000000000000, 0.000000000000000000 ) ) ;
#13249=ORIENTED_EDGE ( 'NONE', *, *, #115942, .T. ) ;
#13250=DIRECTION ( 'NONE',  ( -0.7071067811865486830, -0.7071067811865464625, -0.000000000000000000 ) ) ;
#13251=ORIENTED_EDGE ( 'NONE', *, *, #53464, .F. ) ;
#13252=CARTESIAN_POINT ( 'NONE',  ( 33.70710678118631165, -0.7407075233842788098, 5.000000000000000000 ) ) ;
#13253=DIRECTION ( 'NONE',  ( 0.7071067811865486830, -0.7071067811865464625, -0.000000000000000000 ) ) ;
#13254=VECTOR ( 'NONE', #24625, 1000.000000000000000 ) ;
#13255=LINE ( 'NONE', #104571, #127572 ) ;
#13256=AXIS2_PLACEMENT_3D ( 'NONE', #123861, #134007, #2005 ) ;
#13257=FACE_BOUND ( 'NONE', #32729, .T. ) ;
#13258=DIRECTION ( 'NONE',  ( -0.7071067811865486830, -0.7071067811865464625, 0.000000000000000000 ) ) ;
#13260=CARTESIAN_POINT ( 'NONE',  ( 39.18398860626899705, 28.73617430169814568, 5.000000000000000000 ) ) ;
#13263=CARTESIAN_POINT ( 'NONE',  ( -0.1839886062690032631, 28.73617430169787568, 5.000000000000000000 ) ) ;
#13264=EDGE_LOOP ( 'NONE', ( #109776, #64946, #87468, #112804 ) ) ;
#13265=EDGE_CURVE ( 'NONE', #67219, #58219, #3584, .T. ) ;
#13266=EDGE_CURVE ( 'NONE', #10862, #55621, #71040, .T. ) ;
#13267=VERTEX_POINT ( 'NONE', #18016 ) ;
#13269=ORIENTED_EDGE ( 'NONE', *, *, #62855, .T. ) ;
#13270=VECTOR ( 'NONE', #56838, 1000.000000000000000 ) ;
#13273=FACE_OUTER_BOUND ( 'NONE', #72521, .T. ) ;
#13274=EDGE_CURVE ( 'NONE', #128563, #118592, #71751, .T. ) ;
#13275=CARTESIAN_POINT ( 'NONE',  ( 30.79333936457826937, 21.75929247661550647, 4.998822639870708073 ) ) ;
#13276=VECTOR ( 'NONE', #46055, 1000.000000000000000 ) ;
#13277=DIRECTION ( 'NONE',  ( -0.6830127018922181881, 0.6830127018922202975, -0.2588190451025214056 ) ) ;
#13282=CARTESIAN_POINT ( 'NONE',  ( -21.18398860626899349, 28.73617430169802134, 5.000000000000000000 ) ) ;
#13283=ORIENTED_EDGE ( 'NONE', *, *, #309, .F. ) ;
#13284=ORIENTED_EDGE ( 'NONE', *, *, #72861, .F. ) ;
#13285=CARTESIAN_POINT ( 'NONE',  ( -18.40295003975137078, -2.759949774800250832, 4.658785122533365630 ) ) ;
#13286=VECTOR ( 'NONE', #79707, 1000.000000000000000 ) ;
#13287=VERTEX_POINT ( 'NONE', #4256 ) ;
#13288=ORIENTED_EDGE ( 'NONE', *, *, #62660, .T. ) ;
#13290=ORIENTED_EDGE ( 'NONE', *, *, #117163, .T. ) ;
#13291=DIRECTION ( 'NONE',  ( 0.3543493200069162685, -0.000000000000000000, -0.9351131265310288487 ) ) ;
#13293=DIRECTION ( 'NONE',  ( -0.7071067811865487940, 0.7071067811865463515, -0.000000000000000000 ) ) ;
#13294=ORIENTED_EDGE ( 'NONE', *, *, #6635, .F. ) ;
#13295=FACE_OUTER_BOUND ( 'NONE', #32269, .T. ) ;
#13296=VECTOR ( 'NONE', #62173, 1000.000000000000000 ) ;
#13297=AXIS2_PLACEMENT_3D ( 'NONE', #79669, #112943, #70216 ) ;
#13299=AXIS2_PLACEMENT_3D ( 'NONE', #133962, #23782, #100634 ) ;
#13302=VERTEX_POINT ( 'NONE', #26095 ) ;
#13303=FACE_OUTER_BOUND ( 'NONE', #65799, .T. ) ;
#13305=EDGE_CURVE ( 'NONE', #110282, #92427, #137719, .T. ) ;
#13306=VECTOR ( 'NONE', #92574, 1000.000000000000227 ) ;
#13307=LINE ( 'NONE', #77884, #12790 ) ;
#13308=CARTESIAN_POINT ( 'NONE',  ( -2.510786437626908008, -27.52281430457053446, 5.000000000000000000 ) ) ;
#13309=VERTEX_POINT ( 'NONE', #104329 ) ;
#13310=ORIENTED_EDGE ( 'NONE', *, *, #67677, .T. ) ;
#13311=LINE ( 'NONE', #56175, #21827 ) ;
#13312=CARTESIAN_POINT ( 'NONE',  ( -6.717577386425628738, -21.73023691814492508, 5.000000000000000888 ) ) ;
#13314=ORIENTED_EDGE ( 'NONE', *, *, #130042, .F. ) ;
#13315=CARTESIAN_POINT ( 'NONE',  ( -35.99451991528749772, 28.92564299267963079, 4.000000000000000000 ) ) ;
#13316=LINE ( 'NONE', #1705, #122002 ) ;
#13319=LINE ( 'NONE', #133710, #3194 ) ;
#13320=PLANE ( 'NONE',  #80913 ) ;
#13321=DIRECTION ( 'NONE',  ( 0.6830127018922181881, 0.6830127018922202975, -0.2588190451025214056 ) ) ;
#13322=CARTESIAN_POINT ( 'NONE',  ( -2.671830600776449405, -15.74070752338412404, 4.000000000000000000 ) ) ;
#13323=EDGE_CURVE ( 'NONE', #116320, #71524, #115910, .T. ) ;
#13324=CARTESIAN_POINT ( 'NONE',  ( -29.99999999999979750, -0.2811185226894580280, -5.995736974527445362 ) ) ;
#13325=DIRECTION ( 'NONE',  ( -0.3543493200069162685, -0.000000000000000000, -0.9351131265310288487 ) ) ;
#13326=EDGE_CURVE ( 'NONE', #137801, #100474, #81198, .T. ) ;
#13327=EDGE_CURVE ( 'NONE', #119026, #81137, #115189, .T. ) ;
#13328=ORIENTED_EDGE ( 'NONE', *, *, #131117, .T. ) ;
#13332=ADVANCED_FACE ( 'NONE', ( #72490 ), #138418, .F. ) ;
#13333=CARTESIAN_POINT ( 'NONE',  ( -5.999999999999960032, -16.60178936734449096, 0.8616154019347350701 ) ) ;
#13334=( BOUNDED_CURVE ( )  B_SPLINE_CURVE ( 3, ( #120321, #76896, #87029, #121069 ),
 .UNSPECIFIED., .F., .T. ) 
 B_SPLINE_CURVE_WITH_KNOTS ( ( 4, 4 ),
 ( 1.208578181583248368, 1.359146454359429157 ),
 .UNSPECIFIED. ) 
 CURVE ( )  GEOMETRIC_REPRESENTATION_ITEM ( )  RATIONAL_B_SPLINE_CURVE ( ( 1.000000000000000000, 0.9981116584018958626, 0.9981116584018958626, 1.000000000000000000 ) ) 
 REPRESENTATION_ITEM ( '' )  );
#13336=EDGE_CURVE ( 'NONE', #65177, #46312, #92749, .T. ) ;
#13338=LINE ( 'NONE', #57607, #133906 ) ;
#13339=ORIENTED_EDGE ( 'NONE', *, *, #140049, .T. ) ;
#13340=FACE_OUTER_BOUND ( 'NONE', #112986, .T. ) ;
#13341=CARTESIAN_POINT ( 'NONE',  ( 45.18398860626900415, 28.73617430169818832, 5.000000000000000000 ) ) ;
#13342=CARTESIAN_POINT ( 'NONE',  ( -10.64175702458853401, 15.75929247661555799, 19.34181609438702054 ) ) ;
#13343=VERTEX_POINT ( 'NONE', #59459 ) ;
#13344=ADVANCED_FACE ( 'NONE', ( #81936 ), #105749, .F. ) ;
#13345=DIRECTION ( 'NONE',  ( -0.000000000000000000, -0.3543493200069152693, 0.9351131265310292928 ) ) ;
#13346=LINE ( 'NONE', #46025, #72447 ) ;
#13349=CARTESIAN_POINT ( 'NONE',  ( 3.489213562373097322, -27.52281430457057709, 5.000000000000000000 ) ) ;
#13351=FACE_OUTER_BOUND ( 'NONE', #65865, .T. ) ;
#13352=CARTESIAN_POINT ( 'NONE',  ( 14.99451991528749595, 28.92564299267948513, 4.000000000000000000 ) ) ;
#13353=ORIENTED_EDGE ( 'NONE', *, *, #65784, .F. ) ;
#13355=VERTEX_POINT ( 'NONE', #86897 ) ;
#13356=LINE ( 'NONE', #57625, #22250 ) ;
#13357=ADVANCED_FACE ( 'NONE', ( #130409 ), #29629, .F. ) ;
#13358=FACE_OUTER_BOUND ( 'NONE', #47111, .T. ) ;
#13361=CARTESIAN_POINT ( 'NONE',  ( 26.27718569542921401, -21.72499999999999432, 5.000000000000000000 ) ) ;
#13362=ORIENTED_EDGE ( 'NONE', *, *, #107026, .F. ) ;
#13363=VERTEX_POINT ( 'NONE', #120184 ) ;
#13364=LINE ( 'NONE', #2480, #113486 ) ;
#13366=EDGE_CURVE ( 'NONE', #46544, #38617, #122978, .T. ) ;
#13367=CARTESIAN_POINT ( 'NONE',  ( 45.29974487139158867, -27.71228299555237840, 4.000000000000000000 ) ) ;
#13370=FACE_OUTER_BOUND ( 'NONE', #90331, .T. ) ;
#13371=LINE ( 'NONE', #35182, #124786 ) ;
#13372=ORIENTED_EDGE ( 'NONE', *, *, #12758, .F. ) ;
#13373=VECTOR ( 'NONE', #56323, 1000.000000000000000 ) ;
#13375=FACE_OUTER_BOUND ( 'NONE', #66691, .T. ) ;
#13376=PLANE ( 'NONE',  #136487 ) ;
#13377=CARTESIAN_POINT ( 'NONE',  ( -48.48921356237309510, -27.52281430457089328, 5.000000000000000000 ) ) ;
#13378=EDGE_CURVE ( 'NONE', #16426, #68681, #80355, .T. ) ;
#13379=ORIENTED_EDGE ( 'NONE', *, *, #91759, .F. ) ;
#13380=CARTESIAN_POINT ( 'NONE',  ( -12.18398860626900060, 28.73617430169795739, 5.000000000000000000 ) ) ;
#13382=VECTOR ( 'NONE', #141609, 1000.000000000000000 ) ;
#13385=EDGE_CURVE ( 'NONE', #26526, #73071, #43387, .T. ) ;
#13387=ORIENTED_EDGE ( 'NONE', *, *, #103654, .F. ) ;
#13388=ORIENTED_EDGE ( 'NONE', *, *, #103315, .T. ) ;
#13389=EDGE_CURVE ( 'NONE', #85582, #82671, #63024, .T. ) ;
#13390=CARTESIAN_POINT ( 'NONE',  ( -51.48921356237309510, -27.52281430457091460, 5.000000000000000000 ) ) ;
#13391=DIRECTION ( 'NONE',  ( 0.7071067811865487940, 0.7071067811865463515, 0.000000000000000000 ) ) ;
#13392=VECTOR ( 'NONE', #35072, 1000.000000000000000 ) ;
#13393=LINE ( 'NONE', #56266, #46606 ) ;
#13395=EDGE_LOOP ( 'NONE', ( #13070, #40647, #92582, #72225 ) ) ;
#13396=PLANE ( 'NONE',  #97013 ) ;
#13397=DIRECTION ( 'NONE',  ( 0.3543493200069162685, -0.000000000000000000, -0.9351131265310288487 ) ) ;
#13399=VECTOR ( 'NONE', #53809, 1000.000000000000000 ) ;
#13401=ORIENTED_EDGE ( 'NONE', *, *, #103404, .F. ) ;
#13402=EDGE_LOOP ( 'NONE', ( #108890, #22579, #137519, #92782 ) ) ;
#13404=ORIENTED_EDGE ( 'NONE', *, *, #50372, .T. ) ;
#13405=EDGE_CURVE ( 'NONE', #28845, #60521, #66576, .T. ) ;
#13406=LINE ( 'NONE', #113444, #8200 ) ;
#13407=DIRECTION ( 'NONE',  ( -0.000000000000000000, -0.3543493200069152693, 0.9351131265310292928 ) ) ;
#13408=CARTESIAN_POINT ( 'NONE',  ( -72.29974487139158157, -27.71228299555256669, 4.000000000000000000 ) ) ;
#13409=DIRECTION ( 'NONE',  ( -0.6830127018922181881, 0.6830127018922202975, -0.2588190451025214056 ) ) ;
#13410=LINE ( 'NONE', #3258, #96377 ) ;
#13411=ORIENTED_EDGE ( 'NONE', *, *, #24714, .F. ) ;
#13412=VERTEX_POINT ( 'NONE', #112223 ) ;
#13413=CARTESIAN_POINT ( 'NONE',  ( -8.671830600776404552, 20.25929247661551003, 4.000000000000000000 ) ) ;
#13415=EDGE_CURVE ( 'NONE', #108674, #132815, #133272, .T. ) ;
#13416=EDGE_LOOP ( 'NONE', ( #50129, #59476, #64925, #89276, #78111 ) ) ;
#13417=DIRECTION ( 'NONE',  ( 0.7071067811865487940, -0.7071067811865463515, 0.000000000000000000 ) ) ;
#13419=VECTOR ( 'NONE', #81506, 1000.000000000000227 ) ;
#13420=FACE_BOUND ( 'NONE', #37603, .T. ) ;
#13421=LINE ( 'NONE', #111325, #135827 ) ;
#13422=EDGE_CURVE ( 'NONE', #87748, #141528, #45564, .T. ) ;
#13423=DIRECTION ( 'NONE',  ( -0.6830127018922181881, 0.6830127018922202975, -0.2588190451025214056 ) ) ;
#13424=DIRECTION ( 'NONE',  ( -0.7071067811865486830, -0.7071067811865464625, -0.000000000000000000 ) ) ;
#13425=VECTOR ( 'NONE', #100850, 999.9999999999998863 ) ;
#13426=DIRECTION ( 'NONE',  ( -0.7071067811865486830, -0.7071067811865464625, 0.000000000000000000 ) ) ;
#13427=LINE ( 'NONE', #12729, #4909 ) ;
#13429=ORIENTED_EDGE ( 'NONE', *, *, #132764, .T. ) ;
#13430=EDGE_CURVE ( 'NONE', #76656, #34219, #99157, .T. ) ;
#13434=CARTESIAN_POINT ( 'NONE',  ( -25.17183060077628909, 18.75929247661552068, 4.000000000000000000 ) ) ;
#13437=AXIS2_PLACEMENT_3D ( 'NONE', #138485, #94247, #139215 ) ;
#13438=EDGE_CURVE ( 'NONE', #32782, #29397, #1964, .T. ) ;
#13439=CARTESIAN_POINT ( 'NONE',  ( 6.793339364578431017, 21.75929247661549226, 4.998822639870705409 ) ) ;
#13440=VECTOR ( 'NONE', #76512, 1000.000000000000000 ) ;
#13441=CARTESIAN_POINT ( 'NONE',  ( 24.32816939922335564, -9.740707523384184441, 4.000000000000000000 ) ) ;
#13443=VERTEX_POINT ( 'NONE', #33953 ) ;
#13444=CARTESIAN_POINT ( 'NONE',  ( 12.93606151716249819, -22.22500000000000142, 23.13634534928430142 ) ) ;
#13446=CARTESIAN_POINT ( 'NONE',  ( 63.18398860626900415, 28.73617430169831621, 5.000000000000000000 ) ) ;
#13447=CARTESIAN_POINT ( 'NONE',  ( 20.99999999999985789, 16.55218569542900298, 5.000000000000000000 ) ) ;
#13448=PLANE ( 'NONE',  #98329 ) ;
#13449=DIRECTION ( 'NONE',  ( -0.6830127018922181881, 0.6830127018922202975, -0.2588190451025214056 ) ) ;
#13451=VERTEX_POINT ( 'NONE', #91206 ) ;
#13452=CARTESIAN_POINT ( 'NONE',  ( -15.70710678118643422, 14.25929247661557042, 5.000000000000000000 ) ) ;
#13453=PLANE ( 'NONE',  #106704 ) ;
#13454=EDGE_LOOP ( 'NONE', ( #138559, #99954, #53899, #29412 ) ) ;
#13455=ORIENTED_EDGE ( 'NONE', *, *, #135501, .T. ) ;
#13459=ORIENTED_EDGE ( 'NONE', *, *, #44846, .F. ) ;
#13462=CARTESIAN_POINT ( 'NONE',  ( 0.000000000000000000, 21.72500000000000142, 4.500000000000000888 ) ) ;
#13464=CARTESIAN_POINT ( 'NONE',  ( -27.48921356237309155, -27.52281430457074762, 5.000000000000000000 ) ) ;
#13465=ORIENTED_EDGE ( 'NONE', *, *, #27781, .F. ) ;
#13466=DIRECTION ( 'NONE',  ( -0.3543493200069162685, -0.000000000000000000, -0.9351131265310288487 ) ) ;
#13469=PLANE ( 'NONE',  #25923 ) ;
#13470=LINE ( 'NONE', #92470, #129347 ) ;
#13473=LINE ( 'NONE', #2612, #119764 ) ;
#13474=ORIENTED_EDGE ( 'NONE', *, *, #136171, .T. ) ;
#13475=ORIENTED_EDGE ( 'NONE', *, *, #46296, .T. ) ;
#13478=LINE ( 'NONE', #89644, #23933 ) ;
#13479=AXIS2_PLACEMENT_3D ( 'NONE', #99763, #111342, #434 ) ;
#13480=VECTOR ( 'NONE', #76851, 1000.000000000000000 ) ;
#13481=EDGE_CURVE ( 'NONE', #15939, #27153, #110742, .T. ) ;
#13482=DIRECTION ( 'NONE',  ( -0.7071067811865486830, -0.7071067811865464625, 0.000000000000000000 ) ) ;
#13483=CARTESIAN_POINT ( 'NONE',  ( -21.29974487139158512, -27.71228299555221142, 4.000000000000000000 ) ) ;
#13484=DIRECTION ( 'NONE',  ( 0.6830127018922180770, -0.6830127018922204085, -0.2588190451025213501 ) ) ;
#13485=VECTOR ( 'NONE', #127092, 1000.000000000000000 ) ;
#13486=EDGE_CURVE ( 'NONE', #17086, #63012, #46276, .T. ) ;
#13487=EDGE_CURVE ( 'NONE', #131139, #687, #88705, .T. ) ;
#13488=CARTESIAN_POINT ( 'NONE',  ( -7.499999999999944045, -4.533600742197697819, 5.000000000000000000 ) ) ;
#13489=ORIENTED_EDGE ( 'NONE', *, *, #121448, .F. ) ;
#13490=AXIS2_PLACEMENT_3D ( 'NONE', #41296, #55778, #30440 ) ;
#13491=VECTOR ( 'NONE', #70919, 1000.000000000000000 ) ;
#13493=EDGE_CURVE ( 'NONE', #85379, #74078, #90461, .T. ) ;
#13494=EDGE_CURVE ( 'NONE', #22682, #130801, #112919, .T. ) ;
#13496=CARTESIAN_POINT ( 'NONE',  ( 72.18398860626899705, 28.73617430169837661, 5.000000000000000000 ) ) ;
#13497=EDGE_CURVE ( 'NONE', #136694, #78508, #13579, .T. ) ;
#13498=CARTESIAN_POINT ( 'NONE',  ( 33.48921356237309510, -27.52281430457078670, 5.000000000000000000 ) ) ;
#13499=CARTESIAN_POINT ( 'NONE',  ( 48.18398860626899705, 28.73617430169820608, 5.000000000000000000 ) ) ;
#13503=ORIENTED_EDGE ( 'NONE', *, *, #133305, .F. ) ;
#13505=VECTOR ( 'NONE', #56740, 1000.000000000000000 ) ;
#13506=EDGE_CURVE ( 'NONE', #18584, #19349, #12170, .T. ) ;
#13508=PLANE ( 'NONE',  #36640 ) ;
#13510=EDGE_CURVE ( 'NONE', #54672, #9777, #115023, .T. ) ;
#13511=VECTOR ( 'NONE', #11379, 1000.000000000000000 ) ;
#13512=CARTESIAN_POINT ( 'NONE',  ( -14.39158342593604623, -0.5643469832421014187, 4.274152510792116111 ) ) ;
#13514=FACE_OUTER_BOUND ( 'NONE', #96052, .T. ) ;
#13515=DIRECTION ( 'NONE',  ( -0.7071067811865486830, 0.7071067811865464625, 0.000000000000000000 ) ) ;
#13516=CYLINDRICAL_SURFACE ( 'NONE', #95064, 0.5000000000000004441 ) ;
#13517=EDGE_LOOP ( 'NONE', ( #110209, #93539, #19478, #104709 ) ) ;
#13518=VECTOR ( 'NONE', #72454, 1000.000000000000000 ) ;
#13520=VERTEX_POINT ( 'NONE', #4815 ) ;
#13522=EDGE_CURVE ( 'NONE', #7112, #102959, #136811, .T. ) ;
#13523=VECTOR ( 'NONE', #44932, 999.9999999999998863 ) ;
#13524=CARTESIAN_POINT ( 'NONE',  ( 30.32816939922332367, -18.74070752338408852, 4.000000000000000000 ) ) ;
#13525=LINE ( 'NONE', #25855, #25600 ) ;
#13526=ORIENTED_EDGE ( 'NONE', *, *, #45308, .T. ) ;
#13527=CARTESIAN_POINT ( 'NONE',  ( -3.707106781186516375, 2.259292476615692546, 5.000000000000000000 ) ) ;
#13528=ORIENTED_EDGE ( 'NONE', *, *, #93165, .F. ) ;
#13529=PLANE ( 'NONE',  #39207 ) ;
#13531=DIRECTION ( 'NONE',  ( 0.7071067811865487940, -0.7071067811865463515, 0.000000000000000000 ) ) ;
#13532=EDGE_LOOP ( 'NONE', ( #11932, #6846, #128096, #1458 ) ) ;
#13533=EDGE_CURVE ( 'NONE', #74042, #98919, #91874, .T. ) ;
#13534=DIRECTION ( 'NONE',  ( -0.7071067811865487940, 0.7071067811865463515, -0.000000000000000000 ) ) ;
#13536=CARTESIAN_POINT ( 'NONE',  ( -1.828169399223514624, 0.7592924766157069794, 4.000000000000000000 ) ) ;
#13537=LINE ( 'NONE', #14978, #64451 ) ;
#13539=FACE_OUTER_BOUND ( 'NONE', #116193, .T. ) ;
#13540=PLANE ( 'NONE',  #63539 ) ;
#13541=CARTESIAN_POINT ( 'NONE',  ( -32.99999999999976552, 10.21212019023806938, -2.019456568337719915 ) ) ;
#13544=VECTOR ( 'NONE', #32260, 1000.000000000000000 ) ;
#13545=FACE_OUTER_BOUND ( 'NONE', #40539, .T. ) ;
#13546=DIRECTION ( 'NONE',  ( 0.7071067811865487940, 0.7071067811865463515, 0.000000000000000000 ) ) ;
#13547=VERTEX_POINT ( 'NONE', #114347 ) ;
#13549=CARTESIAN_POINT ( 'NONE',  ( 17.99451991528748351, 28.92564299267950645, 4.000000000000000000 ) ) ;
#13550=EDGE_CURVE ( 'NONE', #99716, #118694, #44247, .T. ) ;
#13551=EDGE_LOOP ( 'NONE', ( #132819, #88899, #28444, #37610 ) ) ;
#13553=ADVANCED_FACE ( 'NONE', ( #92571 ), #82447, .F. ) ;
#13554=CARTESIAN_POINT ( 'NONE',  ( -18.48921356237309510, -27.52281430457068367, 5.000000000000000000 ) ) ;
#13555=FACE_OUTER_BOUND ( 'NONE', #63579, .T. ) ;
#13556=CARTESIAN_POINT ( 'NONE',  ( -18.70679250724062470, 20.25929247661551358, 20.83292124670819234 ) ) ;
#13557=LINE ( 'NONE', #80299, #73379 ) ;
#13558=ORIENTED_EDGE ( 'NONE', *, *, #102914, .T. ) ;
#13559=CARTESIAN_POINT ( 'NONE',  ( 2.287690060339692355, -21.73547319004781286, 4.999917730833664642 ) ) ;
#13560=EDGE_CURVE ( 'NONE', #65963, #124966, #136096, .T. ) ;
#13561=DIRECTION ( 'NONE',  ( 0.7071067811865486830, 0.7071067811865464625, 0.000000000000000000 ) ) ;
#13562=ORIENTED_EDGE ( 'NONE', *, *, #58347, .F. ) ;
#13563=CARTESIAN_POINT ( 'NONE',  ( -19.49999999999986855, 18.43112307739199451, 4.000000000000000000 ) ) ;
#13564=CARTESIAN_POINT ( 'NONE',  ( -54.48921356237310221, -27.52281430457093236, 5.000000000000000000 ) ) ;
#13565=CARTESIAN_POINT ( 'NONE',  ( 4.499999999999979572, -17.94781430457064531, 5.000000000000000000 ) ) ;
#13566=ORIENTED_EDGE ( 'NONE', *, *, #99829, .F. ) ;
#13567=CARTESIAN_POINT ( 'NONE',  ( 8.999999999999941380, 1.931123077392167264, 4.000000000000000000 ) ) ;
#13568=DIRECTION ( 'NONE',  ( -0.000000000000000000, 0.3543493200069153248, 0.9351131265310292928 ) ) ;
#13569=DIRECTION ( 'NONE',  ( 0.6830127018922180770, -0.6830127018922204085, -0.2588190451025213501 ) ) ;
#13570=CARTESIAN_POINT ( 'NONE',  ( -26.52663903635769671, -5.240707523384225297, 16.25846745537489468 ) ) ;
#13573=EDGE_LOOP ( 'NONE', ( #108344, #43238, #31174, #126100 ) ) ;
#13574=ORIENTED_EDGE ( 'NONE', *, *, #58519, .F. ) ;
#13576=EDGE_LOOP ( 'NONE', ( #118429, #140995, #11000, #69061 ) ) ;
#13577=EDGE_CURVE ( 'NONE', #35940, #78703, #137542, .T. ) ;
#13578=DIRECTION ( 'NONE',  ( 0.7071067811865487940, 0.7071067811865463515, 0.000000000000000000 ) ) ;
#13579=LINE ( 'NONE', #2718, #6275 ) ;
#13580=CARTESIAN_POINT ( 'NONE',  ( -11.99999999999991651, -21.41253812416053393, 4.000000000000000000 ) ) ;
#13581=CARTESIAN_POINT ( 'NONE',  ( -51.18398860626899705, 28.73617430169823095, 5.000000000000000000 ) ) ;
#13582=ORIENTED_EDGE ( 'NONE', *, *, #13942, .T. ) ;
#13583=LINE ( 'NONE', #36783, #120852 ) ;
#13584=DIRECTION ( 'NONE',  ( 0.000000000000000000, -0.3543493200069152138, 0.9351131265310292928 ) ) ;
#13587=ORIENTED_EDGE ( 'NONE', *, *, #94600, .F. ) ;
#13588=EDGE_CURVE ( 'NONE', #53081, #25946, #104895, .T. ) ;
#13589=CARTESIAN_POINT ( 'NONE',  ( 24.41161490594814154, 22.22499999999999787, 4.777194822843817690 ) ) ;
#13590=DIRECTION ( 'NONE',  ( -0.7071067811865486830, -0.7071067811865464625, -0.000000000000000000 ) ) ;
#13591=VECTOR ( 'NONE', #70048, 1000.000000000000000 ) ;
#13594=ORIENTED_EDGE ( 'NONE', *, *, #103479, .F. ) ;
#13597=EDGE_CURVE ( 'NONE', #27998, #66021, #115728, .T. ) ;
#13598=CARTESIAN_POINT ( 'NONE',  ( 5.994519915287488843, 28.92564299267942118, 4.000000000000000000 ) ) ;
#13601=LINE ( 'NONE', #124536, #141512 ) ;
#13602=VECTOR ( 'NONE', #31697, 999.9999999999998863 ) ;
#13605=FACE_OUTER_BOUND ( 'NONE', #23511, .T. ) ;
#13606=CARTESIAN_POINT ( 'NONE',  ( 30.48921356237309510, -27.52281430457076894, 5.000000000000000000 ) ) ;
#13608=EDGE_CURVE ( 'NONE', #118125, #129576, #26627, .T. ) ;
#13609=ORIENTED_EDGE ( 'NONE', *, *, #72650, .F. ) ;
#13610=VERTEX_POINT ( 'NONE', #25914 ) ;
#13611=CARTESIAN_POINT ( 'NONE',  ( 9.604862331875157366, 21.75929247661549937, 21.32995629748184641 ) ) ;
#13612=ORIENTED_EDGE ( 'NONE', *, *, #74131, .F. ) ;
#13614=VECTOR ( 'NONE', #106400, 1000.000000000000227 ) ;
#13616=VECTOR ( 'NONE', #141047, 1000.000000000000000 ) ;
#13617=DIRECTION ( 'NONE',  ( 0.7071067811865487940, 0.7071067811865463515, 0.000000000000000000 ) ) ;
#13618=EDGE_CURVE ( 'NONE', #77659, #39354, #49836, .T. ) ;
#13619=EDGE_LOOP ( 'NONE', ( #72457, #112296, #96719, #111880 ) ) ;
#13620=DIRECTION ( 'NONE',  ( -0.000000000000000000, 0.3543493200069153248, 0.9351131265310292928 ) ) ;
#13621=CARTESIAN_POINT ( 'NONE',  ( -21.18398860626899349, 28.73617430169802134, 5.000000000000000000 ) ) ;
#13622=DIRECTION ( 'NONE',  ( -0.6830127018922180770, -0.6830127018922204085, -0.2588190451025213501 ) ) ;
#13623=VECTOR ( 'NONE', #30513, 999.9999999999998863 ) ;
#13624=CARTESIAN_POINT ( 'NONE',  ( 12.32816939922344623, 5.259292476615662792, 4.000000000000000000 ) ) ;
#13625=ORIENTED_EDGE ( 'NONE', *, *, #6036, .T. ) ;
#13628=DIRECTION ( 'NONE',  ( 0.7071067811865487940, 0.7071067811865463515, 0.000000000000000000 ) ) ;
#13629=VECTOR ( 'NONE', #2645, 1000.000000000000000 ) ;
#13630=VERTEX_POINT ( 'NONE', #48375 ) ;
#13632=VERTEX_POINT ( 'NONE', #111975 ) ;
#13633=DIRECTION ( 'NONE',  ( 0.7071067811865487940, 0.7071067811865463515, 0.000000000000000000 ) ) ;
#13634=EDGE_CURVE ( 'NONE', #3834, #52633, #12630, .T. ) ;
#13636=CARTESIAN_POINT ( 'NONE',  ( -26.70025512860841488, -27.71228299555187391, 4.000000000000000000 ) ) ;
#13638=VERTEX_POINT ( 'NONE', #24242 ) ;
#13639=AXIS2_PLACEMENT_3D ( 'NONE', #121768, #22444, #10851 ) ;
#13641=AXIS2_PLACEMENT_3D ( 'NONE', #70418, #106519, #116719 ) ;
#13645=CARTESIAN_POINT ( 'NONE',  ( 24.48921356237309510, -27.52281430457072631, 5.000000000000000000 ) ) ;
#13646=CARTESIAN_POINT ( 'NONE',  ( 24.48921356237309510, -27.52281430457072631, 5.000000000000000000 ) ) ;
#13649=DIRECTION ( 'NONE',  ( -0.6830127018922181881, 0.6830127018922202975, -0.2588190451025214056 ) ) ;
#13650=ORIENTED_EDGE ( 'NONE', *, *, #63274, .T. ) ;
#13651=CARTESIAN_POINT ( 'NONE',  ( 32.20710678118632586, -17.24070752338411339, 5.000000000000000000 ) ) ;
#13652=ORIENTED_EDGE ( 'NONE', *, *, #82126, .F. ) ;
#13653=ORIENTED_EDGE ( 'NONE', *, *, #110640, .F. ) ;
#13654=CARTESIAN_POINT ( 'NONE',  ( 0.2997448713915885632, -27.71228299555206220, 4.000000000000000000 ) ) ;
#13655=ORIENTED_EDGE ( 'NONE', *, *, #49894, .T. ) ;
#13656=DIRECTION ( 'NONE',  ( 0.6830127018922180770, -0.6830127018922204085, -0.2588190451025213501 ) ) ;
#13657=LINE ( 'NONE', #55789, #61718 ) ;
#13658=LINE ( 'NONE', #46366, #3218 ) ;
#13659=CARTESIAN_POINT ( 'NONE',  ( 6.183988606268994381, 28.73617430169791476, 5.000000000000000000 ) ) ;
#13660=ORIENTED_EDGE ( 'NONE', *, *, #10590, .T. ) ;
#13661=ORIENTED_EDGE ( 'NONE', *, *, #82583, .F. ) ;
#13662=CARTESIAN_POINT ( 'NONE',  ( 0.000000000000000000, 0.000000000000000000, 5.000000000000000000 ) ) ;
#13665=ORIENTED_EDGE ( 'NONE', *, *, #35492, .F. ) ;
#13666=ADVANCED_FACE ( 'NONE', ( #24932 ), #25653, .F. ) ;
#13667=LINE ( 'NONE', #90563, #64428 ) ;
#13668=LINE ( 'NONE', #91969, #139147 ) ;
#13669=EDGE_LOOP ( 'NONE', ( #93020, #21787, #28289, #87597 ) ) ;
#13670=ORIENTED_EDGE ( 'NONE', *, *, #86033, .T. ) ;
#13673=LINE ( 'NONE', #91299, #137555 ) ;
#13674=CARTESIAN_POINT ( 'NONE',  ( -30.18398860626900060, 28.73617430169808173, 5.000000000000000000 ) ) ;
#13675=CARTESIAN_POINT ( 'NONE',  ( -63.29974487139158867, -27.71228299555250274, 4.000000000000000000 ) ) ;
#13677=FACE_OUTER_BOUND ( 'NONE', #5112, .T. ) ;
#13678=VERTEX_POINT ( 'NONE', #79380 ) ;
#13679=CARTESIAN_POINT ( 'NONE',  ( -5.999999999999951150, -3.412538124160721331, 4.000000000000000000 ) ) ;
#13680=ADVANCED_FACE ( 'NONE', ( #56899 ), #1720, .F. ) ;
#13681=DIRECTION ( 'NONE',  ( -0.000000000000000000, 0.3543493200069153248, 0.9351131265310292928 ) ) ;
#13682=LINE ( 'NONE', #70293, #113948 ) ;
#13683=ORIENTED_EDGE ( 'NONE', *, *, #110874, .F. ) ;
#13685=VECTOR ( 'NONE', #137254, 1000.000000000000000 ) ;
#13687=VECTOR ( 'NONE', #16242, 999.9999999999998863 ) ;
#13688=DIRECTION ( 'NONE',  ( 0.000000000000000000, 0.000000000000000000, -1.000000000000000000 ) ) ;
#13689=ORIENTED_EDGE ( 'NONE', *, *, #26821, .F. ) ;
#13692=VERTEX_POINT ( 'NONE', #44609 ) ;
#13693=ORIENTED_EDGE ( 'NONE', *, *, #97063, .T. ) ;
#13694=EDGE_CURVE ( 'NONE', #14168, #74087, #114099, .T. ) ;
#13695=PLANE ( 'NONE',  #128026 ) ;
#13696=LINE ( 'NONE', #34784, #110880 ) ;
#13697=ORIENTED_EDGE ( 'NONE', *, *, #121089, .T. ) ;
#13699=ORIENTED_EDGE ( 'NONE', *, *, #81396, .T. ) ;
#13701=CARTESIAN_POINT ( 'NONE',  ( 30.29974487139158867, -27.71228299555227537, 4.000000000000000000 ) ) ;
#13702=LINE ( 'NONE', #57994, #55504 ) ;
#13703=CARTESIAN_POINT ( 'NONE',  ( -20.99451991528748707, 28.92564299267952777, 4.000000000000000000 ) ) ;
#13704=( BOUNDED_CURVE ( )  B_SPLINE_CURVE ( 3, ( #108421, #140378, #9099, #51962 ),
 .UNSPECIFIED., .F., .T. ) 
 B_SPLINE_CURVE_WITH_KNOTS ( ( 4, 4 ),
 ( 5.106027341939279651, 6.645403452391245303 ),
 .UNSPECIFIED. ) 
 CURVE ( )  GEOMETRIC_REPRESENTATION_ITEM ( )  RATIONAL_B_SPLINE_CURVE ( ( 1.000000000000000000, 0.8120851936182276187, 0.8120851936182276187, 1.000000000000000000 ) ) 
 REPRESENTATION_ITEM ( '' )  );
#13705=LINE ( 'NONE', #2848, #21097 ) ;
#13706=CARTESIAN_POINT ( 'NONE',  ( 33.48921356237309510, -27.52281430457078670, 5.000000000000000000 ) ) ;
#13707=CARTESIAN_POINT ( 'NONE',  ( -4.499999999999962697, -4.533600742197694267, 5.000000000000000000 ) ) ;
#13708=CARTESIAN_POINT ( 'NONE',  ( 15.70710678118643422, -12.74070752338415424, 5.000000000000000000 ) ) ;
#13712=CARTESIAN_POINT ( 'NONE',  ( 0.000000000000000000, 0.000000000000000000, 5.000000000000000000 ) ) ;
#13713=VECTOR ( 'NONE', #76362, 999.9999999999998863 ) ;
#13714=DIRECTION ( 'NONE',  ( -0.6830127018922181881, 0.6830127018922202975, -0.2588190451025214056 ) ) ;
#13715=LINE ( 'NONE', #15833, #19949 ) ;
#13716=VERTEX_POINT ( 'NONE', #59057 ) ;
#13717=VERTEX_POINT ( 'NONE', #135855 ) ;
#13719=VERTEX_POINT ( 'NONE', #36538 ) ;
#13721=ORIENTED_EDGE ( 'NONE', *, *, #39600, .T. ) ;
#13724=DIRECTION ( 'NONE',  ( 0.3543493200069162685, -0.000000000000000000, -0.9351131265310288487 ) ) ;
#13726=EDGE_LOOP ( 'NONE', ( #44913, #5156, #131253, #108157 ) ) ;
#13728=CARTESIAN_POINT ( 'NONE',  ( 14.99999999999989342, -16.60178936734447319, 0.8616154019347853632 ) ) ;
#13729=AXIS2_PLACEMENT_3D ( 'NONE', #106239, #96777, #95391 ) ;
#13730=CARTESIAN_POINT ( 'NONE',  ( 26.99999999999981171, 17.96639925780207747, 5.000000000000000000 ) ) ;
#13731=AXIS2_PLACEMENT_3D ( 'NONE', #121059, #100045, #119609 ) ;
#13732=CARTESIAN_POINT ( 'NONE',  ( 10.99806943317893726, -22.22500000000000142, 4.500000000000000888 ) ) ;
#13733=CARTESIAN_POINT ( 'NONE',  ( 14.60438740478481989, -0.8081507193758268315, 4.000000000000000000 ) ) ;
#13734=LINE ( 'NONE', #134867, #67261 ) ;
#13736=DIRECTION ( 'NONE',  ( 0.6830127018922180770, -0.6830127018922204085, -0.2588190451025213501 ) ) ;
#13737=VECTOR ( 'NONE', #35356, 1000.000000000000227 ) ;
#13738=CARTESIAN_POINT ( 'NONE',  ( 27.79289321881326913, -11.24070752338417023, 5.000000000000000000 ) ) ;
#13739=CARTESIAN_POINT ( 'NONE',  ( -29.99451991528749417, 28.92564299267958816, 4.000000000000000000 ) ) ;
#13740=CARTESIAN_POINT ( 'NONE',  ( -9.183988606268997046, 28.73617430169793607, 5.000000000000000000 ) ) ;
#13743=EDGE_CURVE ( 'NONE', #131560, #115494, #19318, .T. ) ;
#13746=ORIENTED_EDGE ( 'NONE', *, *, #135892, .F. ) ;
#13748=ORIENTED_EDGE ( 'NONE', *, *, #2885, .T. ) ;
#13750=FACE_OUTER_BOUND ( 'NONE', #80209, .T. ) ;
#13753=PLANE ( 'NONE',  #5029 ) ;
#13754=LINE ( 'NONE', #102242, #23432 ) ;
#13756=ORIENTED_EDGE ( 'NONE', *, *, #110874, .T. ) ;
#13761=ORIENTED_EDGE ( 'NONE', *, *, #14537, .T. ) ;
#13763=EDGE_CURVE ( 'NONE', #2262, #118592, #30183, .T. ) ;
#13764=ORIENTED_EDGE ( 'NONE', *, *, #22522, .T. ) ;
#13765=DIRECTION ( 'NONE',  ( 0.6830127018922180770, -0.6830127018922204085, -0.2588190451025213501 ) ) ;
#13766=CARTESIAN_POINT ( 'NONE',  ( -24.18398860626899705, 28.73617430169804265, 5.000000000000000000 ) ) ;
#13767=( BOUNDED_CURVE ( )  B_SPLINE_CURVE ( 3, ( #111235, #142474, #9790, #65665 ),
 .UNSPECIFIED., .F., .T. ) 
 B_SPLINE_CURVE_WITH_KNOTS ( ( 4, 4 ),
 ( 2.779374508378134045, 4.199602562396876237 ),
 .UNSPECIFIED. ) 
 CURVE ( )  GEOMETRIC_REPRESENTATION_ITEM ( )  RATIONAL_B_SPLINE_CURVE ( ( 1.000000000000000000, 0.8388583629366543892, 0.8388583629366543892, 1.000000000000000000 ) ) 
 REPRESENTATION_ITEM ( '' )  );
#13769=ORIENTED_EDGE ( 'NONE', *, *, #29455, .F. ) ;
#13770=ORIENTED_EDGE ( 'NONE', *, *, #39705, .T. ) ;
#13771=CARTESIAN_POINT ( 'NONE',  ( 45.18398860626900415, 28.73617430169818832, 5.000000000000000000 ) ) ;
#13772=EDGE_LOOP ( 'NONE', ( #52358, #46249, #62574, #29205 ) ) ;
#13774=VERTEX_POINT ( 'NONE', #86001 ) ;
#13775=PLANE ( 'NONE',  #70291 ) ;
#13776=LINE ( 'NONE', #100821, #75343 ) ;
#13777=CARTESIAN_POINT ( 'NONE',  ( 23.99999999999983302, -15.41253812416059432, 4.000000000000000000 ) ) ;
#13778=EDGE_CURVE ( 'NONE', #125758, #22428, #74433, .T. ) ;
#13779=ORIENTED_EDGE ( 'NONE', *, *, #76318, .F. ) ;
#13780=CARTESIAN_POINT ( 'NONE',  ( 13.49999999999990585, 18.43112307739199451, 4.000000000000000000 ) ) ;
#13781=AXIS2_PLACEMENT_3D ( 'NONE', #73041, #81778, #4837 ) ;
#13782=DIRECTION ( 'NONE',  ( -0.6830127018922180770, 0.6830127018922202975, -0.2588190451025213501 ) ) ;
#13783=VECTOR ( 'NONE', #8638, 1000.000000000000000 ) ;
#13784=VECTOR ( 'NONE', #66157, 999.9999999999998863 ) ;
#13785=VECTOR ( 'NONE', #124076, 1000.000000000000227 ) ;
#13786=PLANE ( 'NONE',  #11964 ) ;
#13787=VECTOR ( 'NONE', #11126, 1000.000000000000000 ) ;
#13788=EDGE_CURVE ( 'NONE', #53159, #36944, #75853, .T. ) ;
#13789=FACE_BOUND ( 'NONE', #134068, .T. ) ;
#13793=FACE_OUTER_BOUND ( 'NONE', #115971, .T. ) ;
#13794=EDGE_CURVE ( 'NONE', #111985, #121113, #13704, .T. ) ;
#13795=VERTEX_POINT ( 'NONE', #109176 ) ;
#13796=CARTESIAN_POINT ( 'NONE',  ( 14.51078643762690490, -27.52281430457045275, 5.000000000000000000 ) ) ;
#13797=ORIENTED_EDGE ( 'NONE', *, *, #45160, .F. ) ;
#13798=VERTEX_POINT ( 'NONE', #120017 ) ;
#13799=VECTOR ( 'NONE', #34790, 999.9999999999998863 ) ;
#13800=ORIENTED_EDGE ( 'NONE', *, *, #139176, .T. ) ;
#13802=ORIENTED_EDGE ( 'NONE', *, *, #7910, .F. ) ;
#13804=DIRECTION ( 'NONE',  ( -0.6830127018922181881, 0.6830127018922202975, -0.2588190451025214056 ) ) ;
#13805=LINE ( 'NONE', #102301, #7977 ) ;
#13806=VERTEX_POINT ( 'NONE', #76582 ) ;
#13808=CARTESIAN_POINT ( 'NONE',  ( -2.700255128608413990, -27.71228299555204089, 4.000000000000000000 ) ) ;
#13810=ADVANCED_FACE ( 'NONE', ( #54820 ), #41790, .F. ) ;
#13811=VECTOR ( 'NONE', #120744, 1000.000000000000227 ) ;
#13812=CARTESIAN_POINT ( 'NONE',  ( 13.99806943317892127, -22.22500000000000142, 4.500000000000000888 ) ) ;
#13813=LINE ( 'NONE', #79869, #30097 ) ;
#13814=DIRECTION ( 'NONE',  ( 0.7071067811865486830, -0.7071067811865464625, -0.000000000000000000 ) ) ;
#13815=CARTESIAN_POINT ( 'NONE',  ( -33.87485380690745274, -14.24070752338413826, 9.401115078912734901 ) ) ;
#13816=VERTEX_POINT ( 'NONE', #96141 ) ;
#13821=CARTESIAN_POINT ( 'NONE',  ( -12.48921356237309155, -27.52281430457064104, 5.000000000000000000 ) ) ;
#13822=VERTEX_POINT ( 'NONE', #53367 ) ;
#13823=VECTOR ( 'NONE', #34258, 1000.000000000000000 ) ;
#13827=FACE_OUTER_BOUND ( 'NONE', #135918, .T. ) ;
#13829=PLANE ( 'NONE',  #16161 ) ;
#13830=ORIENTED_EDGE ( 'NONE', *, *, #64145, .T. ) ;
#13831=VECTOR ( 'NONE', #56247, 1000.000000000000000 ) ;
#13832=DIRECTION ( 'NONE',  ( 0.7071067811865486830, -0.7071067811865464625, -0.000000000000000000 ) ) ;
#13833=EDGE_LOOP ( 'NONE', ( #98500, #8954, #110647, #33143, #86737 ) ) ;
#13834=CARTESIAN_POINT ( 'NONE',  ( -27.29974487139158512, -27.71228299555225405, 4.000000000000000000 ) ) ;
#13836=EDGE_CURVE ( 'NONE', #84892, #51683, #141830, .T. ) ;
#13838=ORIENTED_EDGE ( 'NONE', *, *, #22975, .T. ) ;
#13840=LINE ( 'NONE', #122622, #52241 ) ;
#13841=ADVANCED_FACE ( 'NONE', ( #142542 ), #87445, .T. ) ;
#13844=ORIENTED_EDGE ( 'NONE', *, *, #51208, .F. ) ;
#13845=CARTESIAN_POINT ( 'NONE',  ( 8.671830600776411657, 8.259292476615629042, 4.000000000000000000 ) ) ;
#13846=DIRECTION ( 'NONE',  ( -0.000000000000000000, -0.000000000000000000, 1.000000000000000000 ) ) ;
#13847=ORIENTED_EDGE ( 'NONE', *, *, #101241, .T. ) ;
#13848=CARTESIAN_POINT ( 'NONE',  ( 5.999999999999967137, 2.966399257802236011, 5.000000000000000000 ) ) ;
#13849=DIRECTION ( 'NONE',  ( -0.000000000000000000, -0.3543493200069152693, 0.9351131265310292928 ) ) ;
#13850=PLANE ( 'NONE',  #111809 ) ;
#13852=EDGE_CURVE ( 'NONE', #93313, #129006, #130958, .T. ) ;
#13854=VERTEX_POINT ( 'NONE', #85269 ) ;
#13855=FACE_OUTER_BOUND ( 'NONE', #19886, .T. ) ;
#13856=CARTESIAN_POINT ( 'NONE',  ( -10.17183060077640100, 0.7592924766157104211, 4.000000000000000000 ) ) ;
#13857=LINE ( 'NONE', #110316, #46752 ) ;
#13858=ORIENTED_EDGE ( 'NONE', *, *, #105191, .T. ) ;
#13859=VECTOR ( 'NONE', #35825, 1000.000000000000000 ) ;
#13860=DIRECTION ( 'NONE',  ( 0.7071067811865487940, 0.7071067811865463515, 0.000000000000000000 ) ) ;
#13863=CARTESIAN_POINT ( 'NONE',  ( -18.29974487139159223, -27.71228299555219010, 4.000000000000000000 ) ) ;
#13864=EDGE_LOOP ( 'NONE', ( #84773, #36004, #128833, #14992, #119305 ) ) ;
#13865=EDGE_CURVE ( 'NONE', #64348, #91540, #132404, .T. ) ;
#13866=ORIENTED_EDGE ( 'NONE', *, *, #83858, .F. ) ;
#13868=FACE_OUTER_BOUND ( 'NONE', #82604, .T. ) ;
#13871=VECTOR ( 'NONE', #81301, 1000.000000000000000 ) ;
#13872=ADVANCED_FACE ( 'NONE', ( #18567 ), #62847, .F. ) ;
#13874=EDGE_LOOP ( 'NONE', ( #96226, #119790, #98107, #137963 ) ) ;
#13876=LINE ( 'NONE', #56751, #25879 ) ;
#13878=EDGE_CURVE ( 'NONE', #81140, #63923, #66409, .T. ) ;
#13879=CARTESIAN_POINT ( 'NONE',  ( 21.48921356237309155, -27.52281430457070499, 5.000000000000000000 ) ) ;
#13880=PLANE ( 'NONE',  #103853 ) ;
#13882=DIRECTION ( 'NONE',  ( 1.000000000000000000, 0.000000000000000000, 0.000000000000000000 ) ) ;
#13883=ORIENTED_EDGE ( 'NONE', *, *, #129444, .T. ) ;
#13884=ORIENTED_EDGE ( 'NONE', *, *, #3784, .F. ) ;
#13885=VERTEX_POINT ( 'NONE', #14133 ) ;
#13887=AXIS2_PLACEMENT_3D ( 'NONE', #93389, #71653, #96215 ) ;
#13888=ORIENTED_EDGE ( 'NONE', *, *, #33676, .F. ) ;
#13889=VERTEX_POINT ( 'NONE', #79462 ) ;
#13891=VECTOR ( 'NONE', #932, 1000.000000000000000 ) ;
#13892=ADVANCED_FACE ( 'NONE', ( #89565 ), #91703, .F. ) ;
#13893=CARTESIAN_POINT ( 'NONE',  ( -75.29974487139158157, -27.71228299555258445, 4.000000000000000000 ) ) ;
#13894=DIRECTION ( 'NONE',  ( -0.7071067811865487940, 0.7071067811865463515, 0.000000000000000000 ) ) ;
#13895=VECTOR ( 'NONE', #43633, 999.9999999999998863 ) ;
#13896=VECTOR ( 'NONE', #123932, 1000.000000000000000 ) ;
#13897=VECTOR ( 'NONE', #106563, 1000.000000000000227 ) ;
#13898=ORIENTED_EDGE ( 'NONE', *, *, #42860, .T. ) ;
#13900=CARTESIAN_POINT ( 'NONE',  ( 66.18398860626901126, 28.73617430169833753, 5.000000000000000000 ) ) ;
#13901=VECTOR ( 'NONE', #70, 1000.000000000000000 ) ;
#13902=CARTESIAN_POINT ( 'NONE',  ( 30.48921356237309510, -27.52281430457076894, 5.000000000000000000 ) ) ;
#13903=CARTESIAN_POINT ( 'NONE',  ( 4.637538124160942132, 22.22499999999999432, 4.000000000000000000 ) ) ;
#13905=ORIENTED_EDGE ( 'NONE', *, *, #103565, .T. ) ;
#13906=EDGE_CURVE ( 'NONE', #87654, #60505, #133795, .T. ) ;
#13907=CARTESIAN_POINT ( 'NONE',  ( 18.18398860626898994, 28.73617430169800002, 5.000000000000000000 ) ) ;
#13908=PLANE ( 'NONE',  #30702 ) ;
#13909=DIRECTION ( 'NONE',  ( -0.7071067811865487940, 0.7071067811865463515, -0.000000000000000000 ) ) ;
#13910=AXIS2_PLACEMENT_3D ( 'NONE', #26585, #103407, #4054 ) ;
#13911=CARTESIAN_POINT ( 'NONE',  ( 34.92499999999998295, 20.18441419595452047, 5.773254242255883462 ) ) ;
#13912=DIRECTION ( 'NONE',  ( 0.7071067811865486830, 0.7071067811865463515, 0.000000000000000000 ) ) ;
#13913=DIRECTION ( 'NONE',  ( -0.7071067811865486830, -0.7071067811865464625, -0.000000000000000000 ) ) ;
#13914=PLANE ( 'NONE',  #131494 ) ;
#13916=EDGE_CURVE ( 'NONE', #98260, #97996, #25007, .T. ) ;
#13918=CARTESIAN_POINT ( 'NONE',  ( -28.21498419724172280, -3.740707523384244837, 15.76143240460117489 ) ) ;
#13919=ORIENTED_EDGE ( 'NONE', *, *, #125652, .F. ) ;
#13920=ORIENTED_EDGE ( 'NONE', *, *, #124626, .T. ) ;
#13922=VERTEX_POINT ( 'NONE', #121475 ) ;
#13923=FACE_OUTER_BOUND ( 'NONE', #8894, .T. ) ;
#13924=VECTOR ( 'NONE', #128241, 999.9999999999998863 ) ;
#13925=CARTESIAN_POINT ( 'NONE',  ( -39.18398860626899705, 28.73617430169814568, 5.000000000000000000 ) ) ;
#13926=ORIENTED_EDGE ( 'NONE', *, *, #30115, .F. ) ;
#13927=DIRECTION ( 'NONE',  ( -0.7071067811865487940, 0.7071067811865463515, 0.000000000000000000 ) ) ;
#13932=EDGE_CURVE ( 'NONE', #57920, #12358, #100457, .T. ) ;
#13935=VERTEX_POINT ( 'NONE', #12707 ) ;
#13936=CARTESIAN_POINT ( 'NONE',  ( -7.499999999999944045, 22.22500000000000142, 4.362957392718792349 ) ) ;
#13937=VECTOR ( 'NONE', #39083, 1000.000000000000000 ) ;
#13938=DIRECTION ( 'NONE',  ( -1.000000000000000000, 0.000000000000000000, 0.000000000000000000 ) ) ;
#13939=PLANE ( 'NONE',  #58056 ) ;
#13940=CARTESIAN_POINT ( 'NONE',  ( 34.92499999999998295, 20.81665438641024224, 4.500000000000000888 ) ) ;
#13941=ORIENTED_EDGE ( 'NONE', *, *, #138459, .F. ) ;
#13942=EDGE_CURVE ( 'NONE', #119711, #131795, #46095, .T. ) ;
#13943=ORIENTED_EDGE ( 'NONE', *, *, #92384, .T. ) ;
#13944=VECTOR ( 'NONE', #50459, 1000.000000000000000 ) ;
#13946=DIRECTION ( 'NONE',  ( 0.000000000000000000, 1.000000000000000000, -0.000000000000000000 ) ) ;
#13947=DIRECTION ( 'NONE',  ( -0.7071067811865487940, 0.7071067811865463515, 0.000000000000000000 ) ) ;
#13948=DIRECTION ( 'NONE',  ( 0.7071067811865486830, -0.7071067811865464625, -0.000000000000000000 ) ) ;
#13949=DIRECTION ( 'NONE',  ( -0.7071067811865487940, 0.7071067811865463515, -0.000000000000000000 ) ) ;
#13951=CARTESIAN_POINT ( 'NONE',  ( 54.18398860626899705, 28.73617430169825226, 5.000000000000000000 ) ) ;
#13954=CARTESIAN_POINT ( 'NONE',  ( -29.99999999999979394, -8.731860332648867740, -2.120594902707606533 ) ) ;
#13955=VERTEX_POINT ( 'NONE', #11259 ) ;
#13956=EDGE_CURVE ( 'NONE', #125316, #104580, #99722, .T. ) ;
#13957=VERTEX_POINT ( 'NONE', #393 ) ;
#13958=AXIS2_PLACEMENT_3D ( 'NONE', #29953, #107524, #108202 ) ;
#13959=CARTESIAN_POINT ( 'NONE',  ( 7.171830600776422315, 0.7592924766157069794, 4.000000000000000000 ) ) ;
#13963=ORIENTED_EDGE ( 'NONE', *, *, #88550, .F. ) ;
#13964=PLANE ( 'NONE',  #123314 ) ;
#13965=LINE ( 'NONE', #26306, #80997 ) ;
#13966=VECTOR ( 'NONE', #15097, 1000.000000000000227 ) ;
#13967=DIRECTION ( 'NONE',  ( -0.6830127018922180770, -0.6830127018922204085, -0.2588190451025213501 ) ) ;
#13968=EDGE_CURVE ( 'NONE', #142261, #115779, #3255, .T. ) ;
#13969=FACE_BOUND ( 'NONE', #49679, .T. ) ;
#13970=CARTESIAN_POINT ( 'NONE',  ( -29.99451991528749417, 28.92564299267958816, 4.000000000000000000 ) ) ;
#13972=EDGE_CURVE ( 'NONE', #41631, #42123, #69263, .T. ) ;
#13973=CARTESIAN_POINT ( 'NONE',  ( 26.99451991528749417, 28.92564299267956685, 4.000000000000000000 ) ) ;
#13974=CARTESIAN_POINT ( 'NONE',  ( -39.48921356237310221, -27.52281430457082934, 5.000000000000000000 ) ) ;
#13977=VECTOR ( 'NONE', #116755, 1000.000000000000000 ) ;
#13979=CARTESIAN_POINT ( 'NONE',  ( 9.060110710440143933, -9.740707523384184441, 10.89222023123378591 ) ) ;
#13980=ORIENTED_EDGE ( 'NONE', *, *, #39549, .T. ) ;
#13981=EDGE_LOOP ( 'NONE', ( #7963, #96249, #55701, #136259 ) ) ;
#13985=CARTESIAN_POINT ( 'NONE',  ( -51.48921356237309510, -27.52281430457091460, 5.000000000000000000 ) ) ;
#13986=VERTEX_POINT ( 'NONE', #111303 ) ;
#13987=DIRECTION ( 'NONE',  ( -0.000000000000000000, 0.3543493200069153248, 0.9351131265310292928 ) ) ;
#13989=EDGE_CURVE ( 'NONE', #18457, #131858, #88882, .T. ) ;
#13991=CARTESIAN_POINT ( 'NONE',  ( 13.49999999999991829, -20.94781430457062044, 5.000000000000000000 ) ) ;
#13993=DIRECTION ( 'NONE',  ( -0.7071067811865487940, -0.7071067811865463515, -0.000000000000000000 ) ) ;
#13994=LINE ( 'NONE', #79330, #119943 ) ;
#13995=LINE ( 'NONE', #92273, #92153 ) ;
#13997=LINE ( 'NONE', #102483, #123426 ) ;
#13998=LINE ( 'NONE', #12584, #53235 ) ;
#13999=ORIENTED_EDGE ( 'NONE', *, *, #122910, .T. ) ;
#14000=VECTOR ( 'NONE', #123188, 999.9999999999998863 ) ;
#14001=AXIS2_PLACEMENT_3D ( 'NONE', #133909, #78829, #123039 ) ;
#14002=EDGE_LOOP ( 'NONE', ( #133211, #43593, #38466, #106196 ) ) ;
#14003=VECTOR ( 'NONE', #71941, 1000.000000000000000 ) ;
#14005=FACE_OUTER_BOUND ( 'NONE', #112117, .T. ) ;
#14007=VERTEX_POINT ( 'NONE', #77997 ) ;
#14008=ORIENTED_EDGE ( 'NONE', *, *, #14768, .F. ) ;
#14010=ORIENTED_EDGE ( 'NONE', *, *, #137772, .T. ) ;
#14011=AXIS2_PLACEMENT_3D ( 'NONE', #71024, #84051, #17997 ) ;
#14012=PLANE ( 'NONE',  #2260 ) ;
#14014=EDGE_CURVE ( 'NONE', #133571, #11328, #58425, .T. ) ;
#14016=EDGE_CURVE ( 'NONE', #22013, #108744, #53549, .T. ) ;
#14017=CARTESIAN_POINT ( 'NONE',  ( -6.299744871391586898, -27.71228299555210484, 4.000000000000000000 ) ) ;
#14018=ORIENTED_EDGE ( 'NONE', *, *, #48887, .F. ) ;
#14019=CARTESIAN_POINT ( 'NONE',  ( -34.49999999999976552, -4.216083040037284846, -7.486842126848578083 ) ) ;
#14020=EDGE_CURVE ( 'NONE', #96788, #120651, #122177, .T. ) ;
#14021=DIRECTION ( 'NONE',  ( -0.000000000000000000, 0.3543493200069153248, 0.9351131265310292928 ) ) ;
#14022=VECTOR ( 'NONE', #86837, 1000.000000000000000 ) ;
#14023=LINE ( 'NONE', #135147, #31349 ) ;
#14024=DIRECTION ( 'NONE',  ( -0.6830127018922180770, -0.6830127018922204085, -0.2588190451025213501 ) ) ;
#14025=VERTEX_POINT ( 'NONE', #25733 ) ;
#14026=EDGE_LOOP ( 'NONE', ( #130116, #8122, #5334, #107631 ) ) ;
#14027=LINE ( 'NONE', #67011, #38090 ) ;
#14028=CARTESIAN_POINT ( 'NONE',  ( -35.99451991528749772, 28.92564299267963079, 4.000000000000000000 ) ) ;
#14029=EDGE_CURVE ( 'NONE', #35412, #110682, #16247, .T. ) ;
#14030=EDGE_CURVE ( 'NONE', #37148, #21299, #114169, .T. ) ;
#14031=LINE ( 'NONE', #114077, #118863 ) ;
#14032=EDGE_LOOP ( 'NONE', ( #57574, #61078, #77249, #125256 ) ) ;
#14033=VECTOR ( 'NONE', #29313, 1000.000000000000227 ) ;
#14035=CARTESIAN_POINT ( 'NONE',  ( -17.99999999999987566, 20.70535890316559957, 1.956823837851957792 ) ) ;
#14036=VECTOR ( 'NONE', #82159, 1000.000000000000000 ) ;
#14037=AXIS2_PLACEMENT_3D ( 'NONE', #99486, #10346, #130742 ) ;
#14039=DIRECTION ( 'NONE',  ( 0.3543493200069162685, -0.000000000000000000, -0.9351131265310288487 ) ) ;
#14040=ORIENTED_EDGE ( 'NONE', *, *, #62124, .F. ) ;
#14041=CARTESIAN_POINT ( 'NONE',  ( -24.79289321881327623, 6.759292476615645917, 5.000000000000000000 ) ) ;
#14042=AXIS2_PLACEMENT_3D ( 'NONE', #125725, #59757, #58366 ) ;
#14043=EDGE_CURVE ( 'NONE', #79351, #28576, #92400, .T. ) ;
#14045=DIRECTION ( 'NONE',  ( 0.6830127018922180770, -0.6830127018922204085, -0.2588190451025213501 ) ) ;
#14046=CARTESIAN_POINT ( 'NONE',  ( 22.37176554955601659, -8.240707523384196875, 11.38925528200747372 ) ) ;
#14047=EDGE_CURVE ( 'NONE', #57383, #100719, #114854, .T. ) ;
#14049=ORIENTED_EDGE ( 'NONE', *, *, #13048, .T. ) ;
#14050=VECTOR ( 'NONE', #13345, 1000.000000000000000 ) ;
#14051=EDGE_CURVE ( 'NONE', #84066, #116794, #15531, .T. ) ;
#14052=VERTEX_POINT ( 'NONE', #37340 ) ;
#14054=DIRECTION ( 'NONE',  ( -0.000000000000000000, -0.3543493200069152693, 0.9351131265310292928 ) ) ;
#14055=FACE_OUTER_BOUND ( 'NONE', #70107, .T. ) ;
#14056=DIRECTION ( 'NONE',  ( 0.000000000000000000, 0.000000000000000000, 1.000000000000000000 ) ) ;
#14057=EDGE_CURVE ( 'NONE', #89964, #46947, #3931, .T. ) ;
#14058=AXIS2_PLACEMENT_3D ( 'NONE', #86672, #106231, #32286 ) ;
#14059=DIRECTION ( 'NONE',  ( -0.3543493200069162685, -0.000000000000000000, -0.9351131265310288487 ) ) ;
#14060=DIRECTION ( 'NONE',  ( -0.7071067811865487940, -0.7071067811865463515, -0.000000000000000000 ) ) ;
#14061=EDGE_CURVE ( 'NONE', #79922, #49159, #60547, .T. ) ;
#14064=DIRECTION ( 'NONE',  ( -0.000000000000000000, -0.3543493200069152693, 0.9351131265310292928 ) ) ;
#14066=LINE ( 'NONE', #26400, #118747 ) ;
#14067=ADVANCED_FACE ( 'NONE', ( #26458 ), #138073, .F. ) ;
#14068=LINE ( 'NONE', #68500, #27326 ) ;
#14072=ORIENTED_EDGE ( 'NONE', *, *, #57791, .T. ) ;
#14073=ORIENTED_EDGE ( 'NONE', *, *, #125143, .F. ) ;
#14074=EDGE_CURVE ( 'NONE', #143369, #11170, #51073, .T. ) ;
#14077=CARTESIAN_POINT ( 'NONE',  ( 0.000000000000000000, 0.000000000000000000, 5.000000000000000000 ) ) ;
#14078=CARTESIAN_POINT ( 'NONE',  ( 15.32816939922342669, 20.25929247661551358, 4.000000000000000000 ) ) ;
#14080=CARTESIAN_POINT ( 'NONE',  ( 17.22995720542194675, 21.73644205237997795, 5.000000000000000888 ) ) ;
#14081=DIRECTION ( 'NONE',  ( 0.7071067811865487940, 0.7071067811865463515, -0.000000000000000000 ) ) ;
#14082=VERTEX_POINT ( 'NONE', #117023 ) ;
#14083=ORIENTED_EDGE ( 'NONE', *, *, #8361, .F. ) ;
#14084=CARTESIAN_POINT ( 'NONE',  ( 68.99451991528748351, 28.92564299267986172, 4.000000000000000000 ) ) ;
#14085=DIRECTION ( 'NONE',  ( -0.7071067811865487940, 0.7071067811865463515, 0.000000000000000000 ) ) ;
#14088=VECTOR ( 'NONE', #123445, 999.9999999999998863 ) ;
#14089=CARTESIAN_POINT ( 'NONE',  ( 0.000000000000000000, 0.000000000000000000, 5.000000000000000000 ) ) ;
#14090=CARTESIAN_POINT ( 'NONE',  ( -34.47516574401892342, 12.02806734111569575, 4.998110765256835286 ) ) ;
#14093=ADVANCED_FACE ( 'NONE', ( #17690 ), #71396, .F. ) ;
#14094=DIRECTION ( 'NONE',  ( 1.000000000000000000, 0.000000000000000000, 0.000000000000000000 ) ) ;
#14095=ORIENTED_EDGE ( 'NONE', *, *, #108090, .F. ) ;
#14097=DIRECTION ( 'NONE',  ( -0.6830127018922180770, -0.6830127018922204085, -0.2588190451025213501 ) ) ;
#14098=CARTESIAN_POINT ( 'NONE',  ( -5.816011393731002066, 28.73617430169783304, 5.000000000000000000 ) ) ;
#14099=CARTESIAN_POINT ( 'NONE',  ( 60.29974487139158867, -27.71228299555248142, 4.000000000000000000 ) ) ;
#14101=VECTOR ( 'NONE', #113727, 1000.000000000000000 ) ;
#14102=EDGE_CURVE ( 'NONE', #102488, #10646, #5386, .T. ) ;
#14103=CARTESIAN_POINT ( 'NONE',  ( 9.618384906019905145, -2.240707523384264377, 13.37739548510237242 ) ) ;
#14104=VECTOR ( 'NONE', #80898, 1000.000000000000000 ) ;
#14106=FACE_OUTER_BOUND ( 'NONE', #101461, .T. ) ;
#14108=CARTESIAN_POINT ( 'NONE',  ( 37.58990935480144913, 9.759292476615621936, 11.28811694763787443 ) ) ;
#14109=ORIENTED_EDGE ( 'NONE', *, *, #71373, .T. ) ;
#14110=VECTOR ( 'NONE', #34949, 999.9999999999998863 ) ;
#14112=AXIS2_PLACEMENT_3D ( 'NONE', #31579, #8349, #75804 ) ;
#14113=AXIS2_PLACEMENT_3D ( 'NONE', #70479, #95740, #84867 ) ;
#14114=VECTOR ( 'NONE', #51601, 1000.000000000000227 ) ;
#14115=VECTOR ( 'NONE', #9562, 1000.000000000000227 ) ;
#14116=DIRECTION ( 'NONE',  ( -0.7071067811865486830, -0.7071067811865464625, -0.000000000000000000 ) ) ;
#14117=CARTESIAN_POINT ( 'NONE',  ( 22.82816939922337696, 15.75929247661555976, 4.000000000000000000 ) ) ;
#14118=LINE ( 'NONE', #88866, #122707 ) ;
#14119=CARTESIAN_POINT ( 'NONE',  ( -2.999999999999979128, 16.55218569542900298, 5.000000000000000000 ) ) ;
#14120=CARTESIAN_POINT ( 'NONE',  ( -4.499999999999976019, -9.462702396501018853, -9.474982329943506087 ) ) ;
#14121=ORIENTED_EDGE ( 'NONE', *, *, #79753, .T. ) ;
#14124=CARTESIAN_POINT ( 'NONE',  ( -24.07469600201483928, -0.04978799960962446841, 4.760162856047368329 ) ) ;
#14125=AXIS2_PLACEMENT_3D ( 'NONE', #51232, #15680, #40370 ) ;
#14126=DIRECTION ( 'NONE',  ( -0.3543493200069162685, -0.000000000000000000, -0.9351131265310288487 ) ) ;
#14127=EDGE_LOOP ( 'NONE', ( #42742, #105498, #86359, #59431 ) ) ;
#14128=ORIENTED_EDGE ( 'NONE', *, *, #4066, .T. ) ;
#14130=ORIENTED_EDGE ( 'NONE', *, *, #102636, .F. ) ;
#14131=AXIS2_PLACEMENT_3D ( 'NONE', #102637, #70037, #70737 ) ;
#14132=LINE ( 'NONE', #135245, #24478 ) ;
#14133=CARTESIAN_POINT ( 'NONE',  ( 16.49999999999988276, -11.56887692260769640, 4.000000000000000000 ) ) ;
#14134=DIRECTION ( 'NONE',  ( -0.7071067811865486830, -0.7071067811865464625, 0.000000000000000000 ) ) ;
#14135=AXIS2_PLACEMENT_3D ( 'NONE', #6547, #51555, #70655 ) ;
#14136=CARTESIAN_POINT ( 'NONE',  ( 0.5166543864104510275, 22.22500000000000142, 4.500000000000000888 ) ) ;
#14139=ORIENTED_EDGE ( 'NONE', *, *, #7135, .T. ) ;
#14140=LINE ( 'NONE', #26463, #77022 ) ;
#14141=VECTOR ( 'NONE', #83557, 1000.000000000000000 ) ;
#14142=VERTEX_POINT ( 'NONE', #106118 ) ;
#14143=VECTOR ( 'NONE', #9665, 1000.000000000000000 ) ;
#14144=PLANE ( 'NONE',  #99942 ) ;
#14145=EDGE_CURVE ( 'NONE', #103206, #77014, #115557, .T. ) ;
#14146=ORIENTED_EDGE ( 'NONE', *, *, #12879, .F. ) ;
#14149=FACE_OUTER_BOUND ( 'NONE', #61684, .T. ) ;
#14151=ORIENTED_EDGE ( 'NONE', *, *, #58797, .T. ) ;
#14152=ADVANCED_FACE ( 'NONE', ( #93847 ), #125782, .F. ) ;
#14153=EDGE_CURVE ( 'NONE', #94289, #127411, #70709, .T. ) ;
#14154=FACE_BOUND ( 'NONE', #42195, .T. ) ;
#14155=VECTOR ( 'NONE', #91325, 1000.000000000000000 ) ;
#14156=LINE ( 'NONE', #110597, #6216 ) ;
#14157=DIRECTION ( 'NONE',  ( 0.7071067811865487940, 0.7071067811865463515, 0.000000000000000000 ) ) ;
#14159=CARTESIAN_POINT ( 'NONE',  ( 19.05000000000000071, 3.174999999999997158, 5.000000000000000000 ) ) ;
#14160=EDGE_CURVE ( 'NONE', #3762, #14833, #38760, .T. ) ;
#14164=ORIENTED_EDGE ( 'NONE', *, *, #50279, .F. ) ;
#14165=VECTOR ( 'NONE', #24333, 1000.000000000000000 ) ;
#14166=ORIENTED_EDGE ( 'NONE', *, *, #108460, .F. ) ;
#14168=VERTEX_POINT ( 'NONE', #105424 ) ;
#14169=EDGE_CURVE ( 'NONE', #115165, #46818, #6081, .T. ) ;
#14170=DIRECTION ( 'NONE',  ( -0.7071067811865486830, -0.7071067811865464625, -0.000000000000000000 ) ) ;
#14171=EDGE_LOOP ( 'NONE', ( #128003, #119524, #63939, #19895 ) ) ;
#14172=VECTOR ( 'NONE', #65710, 1000.000000000000000 ) ;
#14173=DIRECTION ( 'NONE',  ( -0.7071067811865487940, 0.7071067811865463515, -0.000000000000000000 ) ) ;
#14175=PLANE ( 'NONE',  #20017 ) ;
#14176=ADVANCED_FACE ( 'NONE', ( #64082 ), #43063, .F. ) ;
#14177=DIRECTION ( 'NONE',  ( -0.7071067811865486830, -0.7071067811865464625, 0.000000000000000000 ) ) ;
#14178=ORIENTED_EDGE ( 'NONE', *, *, #15796, .F. ) ;
#14179=DIRECTION ( 'NONE',  ( -0.3543493200069163240, 0.000000000000000000, 0.9351131265310288487 ) ) ;
#14180=LINE ( 'NONE', #112784, #107941 ) ;
#14182=DIRECTION ( 'NONE',  ( 0.6830127018922181881, 0.6830127018922202975, -0.2588190451025214056 ) ) ;
#14185=DIRECTION ( 'NONE',  ( -0.7071067811865486830, 0.7071067811865464625, 0.000000000000000000 ) ) ;
#14186=ORIENTED_EDGE ( 'NONE', *, *, #32028, .T. ) ;
#14188=LINE ( 'NONE', #102655, #32664 ) ;
#14189=ORIENTED_EDGE ( 'NONE', *, *, #113989, .F. ) ;
#14190=ORIENTED_EDGE ( 'NONE', *, *, #30200, .T. ) ;
#14191=ORIENTED_EDGE ( 'NONE', *, *, #50563, .T. ) ;
#14193=ADVANCED_FACE ( 'NONE', ( #29299 ), #41606, .F. ) ;
#14194=AXIS2_PLACEMENT_3D ( 'NONE', #49977, #134866, #123970 ) ;
#14195=VERTEX_POINT ( 'NONE', #63405 ) ;
#14196=( BOUNDED_CURVE ( )  B_SPLINE_CURVE ( 3, ( #86464, #129957, #141549, #64703 ),
 .UNSPECIFIED., .F., .T. ) 
 B_SPLINE_CURVE_WITH_KNOTS ( ( 4, 4 ),
 ( 2.972453342939734622, 3.211474374380908436 ),
 .UNSPECIFIED. ) 
 CURVE ( )  GEOMETRIC_REPRESENTATION_ITEM ( )  RATIONAL_B_SPLINE_CURVE ( ( 1.000000000000000000, 0.9952447427727515450, 0.9952447427727515450, 1.000000000000000000 ) ) 
 REPRESENTATION_ITEM ( '' )  );
#14199=DIRECTION ( 'NONE',  ( 0.000000000000000000, 0.000000000000000000, -1.000000000000000000 ) ) ;
#14200=ORIENTED_EDGE ( 'NONE', *, *, #43858, .F. ) ;
#14201=PLANE ( 'NONE',  #45680 ) ;
#14202=ADVANCED_FACE ( 'NONE', ( #9680 ), #42352, .T. ) ;
#14203=VERTEX_POINT ( 'NONE', #84433 ) ;
#14204=DIRECTION ( 'NONE',  ( -0.6830127018922180770, -0.6830127018922204085, -0.2588190451025213501 ) ) ;
#14207=ORIENTED_EDGE ( 'NONE', *, *, #112084, .T. ) ;
#14209=CARTESIAN_POINT ( 'NONE',  ( -11.67183060077639212, 14.25929247661557575, 4.000000000000000000 ) ) ;
#14210=EDGE_CURVE ( 'NONE', #60839, #96439, #97389, .T. ) ;
#14211=AXIS2_PLACEMENT_3D ( 'NONE', #70597, #93732, #72017 ) ;
#14212=CARTESIAN_POINT ( 'NONE',  ( -0.7928932188134442116, 12.75929247661558463, 5.000000000000000000 ) ) ;
#14213=ADVANCED_FACE ( 'NONE', ( #119161 ), #98145, .T. ) ;
#14214=VECTOR ( 'NONE', #23439, 1000.000000000000000 ) ;
#14216=CARTESIAN_POINT ( 'NONE',  ( -1.362461875839014791, 22.22500000000000142, 4.000000000000000000 ) ) ;
#14217=ORIENTED_EDGE ( 'NONE', *, *, #87630, .T. ) ;
#14218=ORIENTED_EDGE ( 'NONE', *, *, #102662, .F. ) ;
#14219=ORIENTED_EDGE ( 'NONE', *, *, #87211, .F. ) ;
#14220=DIRECTION ( 'NONE',  ( -0.000000000000000000, -0.3543493200069152693, 0.9351131265310292928 ) ) ;
#14221=VECTOR ( 'NONE', #112326, 1000.000000000000000 ) ;
#14222=AXIS2_PLACEMENT_3D ( 'NONE', #13900, #68354, #56768 ) ;
#14224=AXIS2_PLACEMENT_3D ( 'NONE', #51423, #29633, #118048 ) ;
#14225=EDGE_CURVE ( 'NONE', #137919, #3888, #128626, .T. ) ;
#14226=AXIS2_PLACEMENT_3D ( 'NONE', #64514, #108690, #140632 ) ;
#14228=DIRECTION ( 'NONE',  ( 0.7071067811865487940, 0.7071067811865463515, 0.000000000000000000 ) ) ;
#14230=CARTESIAN_POINT ( 'NONE',  ( -27.48921356237309155, -27.52281430457074762, 5.000000000000000000 ) ) ;
#14231=CARTESIAN_POINT ( 'NONE',  ( -26.20710678118636139, 15.75929247661556687, 5.000000000000000000 ) ) ;
#14232=VECTOR ( 'NONE', #87245, 1000.000000000000000 ) ;
#14233=ORIENTED_EDGE ( 'NONE', *, *, #35438, .T. ) ;
#14234=DIRECTION ( 'NONE',  ( 0.7071067811865486830, -0.7071067811865464625, -0.000000000000000000 ) ) ;
#14236=CARTESIAN_POINT ( 'NONE',  ( -31.82816939922330235, -14.24070752338413648, 4.000000000000000000 ) ) ;
#14237=LINE ( 'NONE', #124427, #127018 ) ;
#14239=EDGE_CURVE ( 'NONE', #43122, #138950, #86563, .T. ) ;
#14240=CARTESIAN_POINT ( 'NONE',  ( -30.48921356237309510, -27.52281430457076894, 5.000000000000000000 ) ) ;
#14241=ORIENTED_EDGE ( 'NONE', *, *, #53020, .T. ) ;
#14242=ORIENTED_EDGE ( 'NONE', *, *, #63952, .T. ) ;
#14243=VERTEX_POINT ( 'NONE', #76399 ) ;
#14245=DIRECTION ( 'NONE',  ( 0.000000000000000000, -1.000000000000000000, 0.000000000000000000 ) ) ;
#14247=CARTESIAN_POINT ( 'NONE',  ( -34.92500000000001137, -22.22500000000000142, 4.500000000000000888 ) ) ;
#14248=ADVANCED_FACE ( 'NONE', ( #130058 ), #140221, .F. ) ;
#14249=LINE ( 'NONE', #2641, #73744 ) ;
#14251=VECTOR ( 'NONE', #74443, 1000.000000000000000 ) ;
#14252=DIRECTION ( 'NONE',  ( -0.7071067811865487940, 0.7071067811865463515, -0.000000000000000000 ) ) ;
#14254=FACE_OUTER_BOUND ( 'NONE', #72038, .T. ) ;
#14256=VECTOR ( 'NONE', #111755, 1000.000000000000000 ) ;
#14258=EDGE_LOOP ( 'NONE', ( #94366, #41111, #119017, #8212 ) ) ;
#14260=VECTOR ( 'NONE', #128923, 1000.000000000000000 ) ;
#14261=ORIENTED_EDGE ( 'NONE', *, *, #34666, .T. ) ;
#14262=FACE_OUTER_BOUND ( 'NONE', #73366, .T. ) ;
#14263=LINE ( 'NONE', #80265, #115808 ) ;
#14264=ORIENTED_EDGE ( 'NONE', *, *, #114991, .T. ) ;
#14265=DIRECTION ( 'NONE',  ( -0.6830127018922181881, 0.6830127018922202975, -0.2588190451025214056 ) ) ;
#14266=CARTESIAN_POINT ( 'NONE',  ( 26.22995720542188991, 21.73644205237998150, 5.000000000000000888 ) ) ;
#14267=ORIENTED_EDGE ( 'NONE', *, *, #137661, .T. ) ;
#14268=CARTESIAN_POINT ( 'NONE',  ( -19.82816939922338761, -17.24070752338410983, 4.000000000000000000 ) ) ;
#14270=LINE ( 'NONE', #93968, #49132 ) ;
#14271=VERTEX_POINT ( 'NONE', #54648 ) ;
#14273=EDGE_CURVE ( 'NONE', #54563, #51456, #19846, .T. ) ;
#14277=ORIENTED_EDGE ( 'NONE', *, *, #117154, .T. ) ;
#14278=DIRECTION ( 'NONE',  ( -0.7071067811865486830, -0.7071067811865464625, 0.000000000000000000 ) ) ;
#14279=FACE_OUTER_BOUND ( 'NONE', #91220, .T. ) ;
#14280=CARTESIAN_POINT ( 'NONE',  ( -23.84387692260742142, -22.22500000000000142, 4.000000000000000000 ) ) ;
#14282=VECTOR ( 'NONE', #132748, 1000.000000000000000 ) ;
#14284=CARTESIAN_POINT ( 'NONE',  ( 12.18398860626900060, 28.73617430169795739, 5.000000000000000000 ) ) ;
#14285=VECTOR ( 'NONE', #29071, 1000.000000000000000 ) ;
#14286=CARTESIAN_POINT ( 'NONE',  ( 0.1839886062690032631, 28.73617430169787568, 5.000000000000000000 ) ) ;
#14287=ORIENTED_EDGE ( 'NONE', *, *, #25908, .T. ) ;
#14291=VECTOR ( 'NONE', #104952, 999.9999999999998863 ) ;
#14292=PLANE ( 'NONE',  #10651 ) ;
#14293=CARTESIAN_POINT ( 'NONE',  ( 12.48921356237309155, -27.52281430457064104, 5.000000000000000000 ) ) ;
#14294=PLANE ( 'NONE',  #58581 ) ;
#14295=VECTOR ( 'NONE', #17603, 1000.000000000000000 ) ;
#14296=CARTESIAN_POINT ( 'NONE',  ( -8.816011393731004731, 28.73617430169781173, 5.000000000000000000 ) ) ;
#14297=VERTEX_POINT ( 'NONE', #118445 ) ;
#14298=CARTESIAN_POINT ( 'NONE',  ( -27.18398860626900060, 28.73617430169806042, 5.000000000000000000 ) ) ;
#14300=LINE ( 'NONE', #15002, #16083 ) ;
#14301=CARTESIAN_POINT ( 'NONE',  ( 45.18398860626900415, 28.73617430169818832, 5.000000000000000000 ) ) ;
#14303=ORIENTED_EDGE ( 'NONE', *, *, #109516, .F. ) ;
#14304=DIRECTION ( 'NONE',  ( 0.7071067811865487940, 0.7071067811865463515, -0.000000000000000000 ) ) ;
#14305=LINE ( 'NONE', #11414, #82280 ) ;
#14307=DIRECTION ( 'NONE',  ( 0.7071067811865487940, 0.7071067811865463515, 0.000000000000000000 ) ) ;
#14308=FACE_OUTER_BOUND ( 'NONE', #62462, .T. ) ;
#14309=VERTEX_POINT ( 'NONE', #108250 ) ;
#14310=EDGE_LOOP ( 'NONE', ( #46702, #44515, #45633, #52805 ) ) ;
#14311=EDGE_LOOP ( 'NONE', ( #3738, #20252, #100141, #130496 ) ) ;
#14313=ORIENTED_EDGE ( 'NONE', *, *, #55459, .F. ) ;
#14314=DIRECTION ( 'NONE',  ( -0.7071067811865486830, -0.7071067811865464625, -0.000000000000000000 ) ) ;
#14315=CARTESIAN_POINT ( 'NONE',  ( -23.99999999999982947, -0.1606350220013114671, 4.664761815935120737 ) ) ;
#14316=DIRECTION ( 'NONE',  ( -0.3543493200069162685, -0.000000000000000000, -0.9351131265310288487 ) ) ;
#14317=CARTESIAN_POINT ( 'NONE',  ( 38.99451991528749062, 28.92564299267965211, 4.000000000000000000 ) ) ;
#14318=ORIENTED_EDGE ( 'NONE', *, *, #136296, .T. ) ;
#14322=DIRECTION ( 'NONE',  ( -0.7071067811865487940, 0.7071067811865463515, 0.000000000000000000 ) ) ;
#14323=VECTOR ( 'NONE', #79536, 1000.000000000000227 ) ;
#14324=DIRECTION ( 'NONE',  ( -0.000000000000000000, 0.3543493200069153248, 0.9351131265310292928 ) ) ;
#14325=VECTOR ( 'NONE', #100133, 999.9999999999998863 ) ;
#14327=ORIENTED_EDGE ( 'NONE', *, *, #78354, .T. ) ;
#14328=CARTESIAN_POINT ( 'NONE',  ( 33.32816939922329880, 17.25929247661554555, 4.000000000000000000 ) ) ;
#14330=VECTOR ( 'NONE', #75826, 1000.000000000000000 ) ;
#14331=DIRECTION ( 'NONE',  ( -0.000000000000000000, -0.3543493200069152693, 0.9351131265310292928 ) ) ;
#14332=DIRECTION ( 'NONE',  ( 0.7071067811865487940, 0.7071067811865463515, -0.000000000000000000 ) ) ;
#14334=VECTOR ( 'NONE', #74440, 999.9999999999998863 ) ;
#14335=EDGE_LOOP ( 'NONE', ( #18034, #129148, #111491, #817 ) ) ;
#14336=EDGE_LOOP ( 'NONE', ( #85534, #1151, #130551, #61330, #21181 ) ) ;
#14337=ADVANCED_FACE ( 'NONE', ( #32164 ), #108983, .F. ) ;
#14338=CARTESIAN_POINT ( 'NONE',  ( -42.48921356237308800, -27.52281430457085065, 5.000000000000000000 ) ) ;
#14339=ADVANCED_FACE ( 'NONE', ( #7532 ), #142371, .F. ) ;
#14340=EDGE_CURVE ( 'NONE', #135705, #117224, #104326, .T. ) ;
#14341=CARTESIAN_POINT ( 'NONE',  ( -8.994519915287490619, 28.92564299267944250, 4.000000000000000000 ) ) ;
#14343=DIRECTION ( 'NONE',  ( 0.7071067811865487940, -0.7071067811865463515, 0.000000000000000000 ) ) ;
#14344=LINE ( 'NONE', #136115, #105793 ) ;
#14345=FACE_OUTER_BOUND ( 'NONE', #32304, .T. ) ;
#14347=EDGE_CURVE ( 'NONE', #53397, #47033, #24852, .T. ) ;
#14348=DIRECTION ( 'NONE',  ( 0.6830127018922181881, 0.6830127018922202975, -0.2588190451025214056 ) ) ;
#14350=ORIENTED_EDGE ( 'NONE', *, *, #106333, .T. ) ;
#14353=ORIENTED_EDGE ( 'NONE', *, *, #68660, .F. ) ;
#14354=VECTOR ( 'NONE', #51293, 1000.000000000000114 ) ;
#14355=EDGE_CURVE ( 'NONE', #96152, #85530, #87972, .T. ) ;
#14357=CARTESIAN_POINT ( 'NONE',  ( 77.99451991528749772, 28.92564299267992567, 4.000000000000000000 ) ) ;
#14358=ORIENTED_EDGE ( 'NONE', *, *, #142085, .F. ) ;
#14359=LINE ( 'NONE', #115766, #96874 ) ;
#14360=CARTESIAN_POINT ( 'NONE',  ( -15.29974487139158867, -27.71228299555216879, 4.000000000000000000 ) ) ;
#14361=VECTOR ( 'NONE', #45634, 1000.000000000000000 ) ;
#14362=LINE ( 'NONE', #136133, #61948 ) ;
#14366=ORIENTED_EDGE ( 'NONE', *, *, #48641, .F. ) ;
#14367=DIRECTION ( 'NONE',  ( 0.7071067811865486830, -0.7071067811865464625, -0.000000000000000000 ) ) ;
#14369=ORIENTED_EDGE ( 'NONE', *, *, #52665, .F. ) ;
#14370=PLANE ( 'NONE',  #48109 ) ;
#14371=ORIENTED_EDGE ( 'NONE', *, *, #68145, .T. ) ;
#14372=ORIENTED_EDGE ( 'NONE', *, *, #69941, .F. ) ;
#14374=VERTEX_POINT ( 'NONE', #23414 ) ;
#14375=VERTEX_POINT ( 'NONE', #35775 ) ;
#14377=EDGE_CURVE ( 'NONE', #138876, #121112, #57511, .T. ) ;
#14378=AXIS2_PLACEMENT_3D ( 'NONE', #28479, #41461, #62535 ) ;
#14379=VERTEX_POINT ( 'NONE', #90854 ) ;
#14380=CARTESIAN_POINT ( 'NONE',  ( 3.299744871391591339, -27.71228299555208352, 4.000000000000000000 ) ) ;
#14381=LINE ( 'NONE', #103504, #49594 ) ;
#14383=LINE ( 'NONE', #102836, #61343 ) ;
#14385=VECTOR ( 'NONE', #44114, 1000.000000000000000 ) ;
#14386=DIRECTION ( 'NONE',  ( -0.7071067811865486830, 0.7071067811865464625, 0.000000000000000000 ) ) ;
#14388=CARTESIAN_POINT ( 'NONE',  ( 1.553349423367815563, 2.259292476615697876, 14.86850063742354067 ) ) ;
#14389=VECTOR ( 'NONE', #58734, 1000.000000000000000 ) ;
#14390=DIRECTION ( 'NONE',  ( -0.3543493200069162685, -0.000000000000000000, -0.9351131265310288487 ) ) ;
#14392=EDGE_CURVE ( 'NONE', #103662, #84513, #22673, .T. ) ;
#14394=LINE ( 'NONE', #101395, #129103 ) ;
#14395=CARTESIAN_POINT ( 'NONE',  ( 34.49999999999975842, 1.464255608400477415, 4.994342998332161443 ) ) ;
#14396=ORIENTED_EDGE ( 'NONE', *, *, #7467, .F. ) ;
#14397=ADVANCED_FACE ( 'NONE', ( #1637 ), #111877, .F. ) ;
#14398=ORIENTED_EDGE ( 'NONE', *, *, #77044, .F. ) ;
#14399=CARTESIAN_POINT ( 'NONE',  ( 30.18398860626900060, 28.73617430169808173, 5.000000000000000000 ) ) ;
#14400=EDGE_LOOP ( 'NONE', ( #23097, #74515, #133501, #65818 ) ) ;
#14401=EDGE_CURVE ( 'NONE', #31895, #68079, #121306, .T. ) ;
#14403=CARTESIAN_POINT ( 'NONE',  ( 33.29974487139158867, -27.71228299555229313, 4.000000000000000000 ) ) ;
#14405=DIRECTION ( 'NONE',  ( -1.000000000000000000, -8.718663809566799855E-16, 0.000000000000000000 ) ) ;
#14406=DIRECTION ( 'NONE',  ( -0.7071067811865486830, 0.7071067811865464625, 0.000000000000000000 ) ) ;
#14408=CARTESIAN_POINT ( 'NONE',  ( 45.18398860626900415, 28.73617430169818832, 5.000000000000000000 ) ) ;
#14409=VECTOR ( 'NONE', #77781, 1000.000000000000000 ) ;
#14410=VERTEX_POINT ( 'NONE', #43756 ) ;
#14411=ADVANCED_FACE ( 'NONE', ( #134349 ), #35047, .F. ) ;
#14412=CARTESIAN_POINT ( 'NONE',  ( -4.499999999999970690, 3.431123077392153053, 4.000000000000000000 ) ) ;
#14414=EDGE_LOOP ( 'NONE', ( #2010, #94234, #111645 ) ) ;
#14417=LINE ( 'NONE', #45651, #23421 ) ;
#14418=EDGE_LOOP ( 'NONE', ( #32748, #99347, #66030 ) ) ;
#14419=VERTEX_POINT ( 'NONE', #55360 ) ;
#14420=ORIENTED_EDGE ( 'NONE', *, *, #50861, .T. ) ;
#14421=DIRECTION ( 'NONE',  ( 0.7071067811865486830, -0.7071067811865464625, -0.000000000000000000 ) ) ;
#14423=AXIS2_PLACEMENT_3D ( 'NONE', #141198, #98426, #86846 ) ;
#14424=AXIS2_PLACEMENT_3D ( 'NONE', #101410, #57957, #68131 ) ;
#14425=PLANE ( 'NONE',  #3376 ) ;
#14426=VECTOR ( 'NONE', #19674, 999.9999999999998863 ) ;
#14427=DIRECTION ( 'NONE',  ( 0.7071067811865487940, -0.7071067811865463515, 0.000000000000000000 ) ) ;
#14428=( BOUNDED_CURVE ( )  B_SPLINE_CURVE ( 3, ( #45353, #54782, #34440, #89529 ),
 .UNSPECIFIED., .F., .F. ) 
 B_SPLINE_CURVE_WITH_KNOTS ( ( 4, 4 ),
 ( 5.920967161967927161, 7.341195215986644484 ),
 .UNSPECIFIED. ) 
 CURVE ( )  GEOMETRIC_REPRESENTATION_ITEM ( )  RATIONAL_B_SPLINE_CURVE ( ( 1.000000000000000000, 0.8388583629366599403, 0.8388583629366599403, 1.000000000000000000 ) ) 
 REPRESENTATION_ITEM ( '' )  );
#14430=CARTESIAN_POINT ( 'NONE',  ( 39.18398860626899705, 28.73617430169814568, 5.000000000000000000 ) ) ;
#14432=CARTESIAN_POINT ( 'NONE',  ( 15.32816939922342137, -18.74070752338409562, 4.000000000000000000 ) ) ;
#14435=LINE ( 'NONE', #104995, #99804 ) ;
#14436=DIRECTION ( 'NONE',  ( -0.000000000000000000, 0.000000000000000000, 1.000000000000000000 ) ) ;
#14437=ORIENTED_EDGE ( 'NONE', *, *, #73781, .F. ) ;
#14439=VECTOR ( 'NONE', #27110, 1000.000000000000000 ) ;
#14441=EDGE_LOOP ( 'NONE', ( #88165, #85452, #4274, #16927 ) ) ;
#14442=FACE_OUTER_BOUND ( 'NONE', #13551, .T. ) ;
#14443=ORIENTED_EDGE ( 'NONE', *, *, #86309, .T. ) ;
#14444=EDGE_CURVE ( 'NONE', #95280, #69167, #11810, .T. ) ;
#14446=DIRECTION ( 'NONE',  ( -0.000000000000000000, 0.000000000000000000, 1.000000000000000000 ) ) ;
#14447=LINE ( 'NONE', #39047, #138667 ) ;
#14448=ORIENTED_EDGE ( 'NONE', *, *, #95271, .T. ) ;
#14450=CARTESIAN_POINT ( 'NONE',  ( 16.04515773336655826, -21.74070752338406365, 21.72585301388588519 ) ) ;
#14451=CARTESIAN_POINT ( 'NONE',  ( 20.99451991528748707, 28.92564299267952777, 4.000000000000000000 ) ) ;
#14452=LINE ( 'NONE', #68173, #122578 ) ;
#14453=DIRECTION ( 'NONE',  ( -0.7071067811865487940, 0.7071067811865463515, 0.000000000000000000 ) ) ;
#14455=DIRECTION ( 'NONE',  ( -0.7071067811865486830, -0.7071067811865464625, 0.000000000000000000 ) ) ;
#14456=LINE ( 'NONE', #58735, #75013 ) ;
#14458=LINE ( 'NONE', #12305, #106910 ) ;
#14459=PLANE ( 'NONE',  #15767 ) ;
#14460=DIRECTION ( 'NONE',  ( -0.7071067811865486830, -0.7071067811865464625, -0.000000000000000000 ) ) ;
#14461=CARTESIAN_POINT ( 'NONE',  ( 0.000000000000000000, 0.000000000000000000, 5.000000000000000000 ) ) ;
#14462=VERTEX_POINT ( 'NONE', #68403 ) ;
#14463=ADVANCED_FACE ( 'NONE', ( #112582 ), #13241, .T. ) ;
#14464=VECTOR ( 'NONE', #66283, 1000.000000000000000 ) ;
#14465=ORIENTED_EDGE ( 'NONE', *, *, #78870, .T. ) ;
#14467=EDGE_CURVE ( 'NONE', #134641, #135641, #36453, .T. ) ;
#14468=ORIENTED_EDGE ( 'NONE', *, *, #42970, .F. ) ;
#14469=ORIENTED_EDGE ( 'NONE', *, *, #127623, .F. ) ;
#14471=LINE ( 'NONE', #127509, #94293 ) ;
#14472=LINE ( 'NONE', #126102, #11631 ) ;
#14473=VECTOR ( 'NONE', #108584, 1000.000000000000000 ) ;
#14475=ORIENTED_EDGE ( 'NONE', *, *, #113763, .F. ) ;
#14476=DIRECTION ( 'NONE',  ( -0.000000000000000000, 0.000000000000000000, 1.000000000000000000 ) ) ;
#14477=DIRECTION ( 'NONE',  ( -0.000000000000000000, 0.3543493200069152138, -0.9351131265310292928 ) ) ;
#14478=PLANE ( 'NONE',  #39518 ) ;
#14481=CARTESIAN_POINT ( 'NONE',  ( -69.48921356237309510, -27.52281430457103895, 5.000000000000000000 ) ) ;
#14482=PLANE ( 'NONE',  #119155 ) ;
#14483=CARTESIAN_POINT ( 'NONE',  ( 31.17183060077626067, -8.240707523384196875, 4.000000000000000000 ) ) ;
#14485=LINE ( 'NONE', #58031, #14512 ) ;
#14486=LINE ( 'NONE', #122517, #40775 ) ;
#14487=CARTESIAN_POINT ( 'NONE',  ( 5.994519915287488843, 28.92564299267942118, 4.000000000000000000 ) ) ;
#14491=ORIENTED_EDGE ( 'NONE', *, *, #108980, .F. ) ;
#14492=AXIS2_PLACEMENT_3D ( 'NONE', #25014, #3262, #12715 ) ;
#14493=DIRECTION ( 'NONE',  ( 0.7071067811865486830, -0.7071067811865464625, -0.000000000000000000 ) ) ;
#14494=AXIS2_PLACEMENT_3D ( 'NONE', #25872, #49804, #93977 ) ;
#14495=CARTESIAN_POINT ( 'NONE',  ( 29.35681257248243980, -20.24070752338406720, 21.22881796311219560 ) ) ;
#14496=ORIENTED_EDGE ( 'NONE', *, *, #28252, .T. ) ;
#14497=CARTESIAN_POINT ( 'NONE',  ( -18.18398860626898994, 28.73617430169800002, 5.000000000000000000 ) ) ;
#14498=CARTESIAN_POINT ( 'NONE',  ( -45.48921356237309510, -27.52281430457087197, 5.000000000000000000 ) ) ;
#14500=ORIENTED_EDGE ( 'NONE', *, *, #45738, .T. ) ;
#14501=EDGE_CURVE ( 'NONE', #53245, #127371, #37900, .T. ) ;
#14502=ORIENTED_EDGE ( 'NONE', *, *, #53805, .F. ) ;
#14503=CARTESIAN_POINT ( 'NONE',  ( 19.05000000000000071, 3.174999999999997158, 4.000000000000000000 ) ) ;
#14504=VECTOR ( 'NONE', #57875, 1000.000000000000000 ) ;
#14505=CARTESIAN_POINT ( 'NONE',  ( -33.98911971346028338, -22.02621442084248216, 4.990779571109225543 ) ) ;
#14506=ORIENTED_EDGE ( 'NONE', *, *, #4183, .F. ) ;
#14507=VERTEX_POINT ( 'NONE', #82829 ) ;
#14508=ORIENTED_EDGE ( 'NONE', *, *, #20555, .F. ) ;
#14509=LINE ( 'NONE', #23969, #49121 ) ;
#14510=EDGE_CURVE ( 'NONE', #86215, #81446, #26994, .T. ) ;
#14512=VECTOR ( 'NONE', #114492, 1000.000000000000000 ) ;
#14513=EDGE_CURVE ( 'NONE', #37639, #106934, #116859, .T. ) ;
#14514=EDGE_CURVE ( 'NONE', #5941, #72014, #59654, .T. ) ;
#14515=CARTESIAN_POINT ( 'NONE',  ( -21.29974487139158512, -27.71228299555221142, 4.000000000000000000 ) ) ;
#14516=EDGE_CURVE ( 'NONE', #86498, #25409, #3096, .T. ) ;
#14517=ORIENTED_EDGE ( 'NONE', *, *, #13506, .T. ) ;
#14518=VERTEX_POINT ( 'NONE', #3770 ) ;
#14519=CARTESIAN_POINT ( 'NONE',  ( -1.499999999999987566, -9.462702396501011748, -9.474982329943509640 ) ) ;
#14521=EDGE_LOOP ( 'NONE', ( #78282, #3813, #30355, #16773 ) ) ;
#14522=EDGE_LOOP ( 'NONE', ( #3302, #58503, #101827, #92395 ) ) ;
#14523=VECTOR ( 'NONE', #77738, 999.9999999999998863 ) ;
#14525=EDGE_CURVE ( 'NONE', #123401, #35122, #81413, .T. ) ;
#14526=VECTOR ( 'NONE', #39211, 1000.000000000000000 ) ;
#14527=CARTESIAN_POINT ( 'NONE',  ( 6.489213562373093325, -27.52281430457059841, 5.000000000000000000 ) ) ;
#14528=AXIS2_PLACEMENT_3D ( 'NONE', #52521, #121344, #22030 ) ;
#14529=ADVANCED_FACE ( 'NONE', ( #5218 ), #135767, .T. ) ;
#14530=FACE_OUTER_BOUND ( 'NONE', #120294, .T. ) ;
#14531=CARTESIAN_POINT ( 'NONE',  ( -17.99999999999987566, -0.2811185226894475919, -5.995736974527472896 ) ) ;
#14532=ORIENTED_EDGE ( 'NONE', *, *, #54480, .F. ) ;
#14533=DIRECTION ( 'NONE',  ( -0.000000000000000000, 0.000000000000000000, 1.000000000000000000 ) ) ;
#14534=VECTOR ( 'NONE', #70607, 1000.000000000000000 ) ;
#14535=AXIS2_PLACEMENT_3D ( 'NONE', #60706, #104874, #5539 ) ;
#14536=DIRECTION ( 'NONE',  ( 0.6830127018922180770, -0.6830127018922204085, -0.2588190451025213501 ) ) ;
#14537=EDGE_CURVE ( 'NONE', #99617, #82100, #72702, .T. ) ;
#14538=FACE_BOUND ( 'NONE', #99936, .T. ) ;
#14541=CARTESIAN_POINT ( 'NONE',  ( -2.999999999999975131, 10.93112307739207267, 4.000000000000000000 ) ) ;
#14542=CARTESIAN_POINT ( 'NONE',  ( 12.48921356237309155, -27.52281430457064104, 5.000000000000000000 ) ) ;
#14544=VERTEX_POINT ( 'NONE', #27702 ) ;
#14545=DIRECTION ( 'NONE',  ( 0.7071067811865487940, 0.7071067811865463515, 0.000000000000000000 ) ) ;
#14547=ORIENTED_EDGE ( 'NONE', *, *, #80357, .F. ) ;
#14548=EDGE_CURVE ( 'NONE', #63812, #76671, #114699, .T. ) ;
#14549=ORIENTED_EDGE ( 'NONE', *, *, #26664, .T. ) ;
#14551=VERTEX_POINT ( 'NONE', #116139 ) ;
#14553=CARTESIAN_POINT ( 'NONE',  ( 15.18398860626900237, 28.73617430169797871, 5.000000000000000000 ) ) ;
#14555=DIRECTION ( 'NONE',  ( 0.7071067811865487940, 0.7071067811865463515, 0.000000000000000000 ) ) ;
#14556=ORIENTED_EDGE ( 'NONE', *, *, #35382, .F. ) ;
#14557=CARTESIAN_POINT ( 'NONE',  ( -34.42500000000001137, -22.22500000000000142, 4.500000000000000888 ) ) ;
#14558=AXIS2_PLACEMENT_3D ( 'NONE', #84649, #73082, #17239 ) ;
#14559=CARTESIAN_POINT ( 'NONE',  ( 29.99999999999979039, 4.931123077392140175, 4.000000000000000000 ) ) ;
#14560=LINE ( 'NONE', #37763, #57882 ) ;
#14563=LINE ( 'NONE', #71111, #14632 ) ;
#14564=VERTEX_POINT ( 'NONE', #61118 ) ;
#14565=EDGE_CURVE ( 'NONE', #116655, #89946, #138629, .T. ) ;
#14566=VERTEX_POINT ( 'NONE', #55724 ) ;
#14567=ORIENTED_EDGE ( 'NONE', *, *, #84109, .F. ) ;
#14568=ORIENTED_EDGE ( 'NONE', *, *, #60003, .T. ) ;
#14569=DIRECTION ( 'NONE',  ( -0.000000000000000000, -0.3543493200069152693, 0.9351131265310292928 ) ) ;
#14570=ORIENTED_EDGE ( 'NONE', *, *, #104781, .T. ) ;
#14571=VERTEX_POINT ( 'NONE', #109369 ) ;
#14572=CARTESIAN_POINT ( 'NONE',  ( 39.18398860626899705, 28.73617430169814568, 5.000000000000000000 ) ) ;
#14573=CARTESIAN_POINT ( 'NONE',  ( -8.939889289559747709, -9.740707523384184441, 10.89222023123382854 ) ) ;
#14574=ORIENTED_EDGE ( 'NONE', *, *, #53157, .F. ) ;
#14576=VERTEX_POINT ( 'NONE', #121655 ) ;
#14577=EDGE_CURVE ( 'NONE', #139420, #72096, #21659, .T. ) ;
#14578=CARTESIAN_POINT ( 'NONE',  ( -4.671406296382802914, 22.22500000000000142, -6.464217593021417407 ) ) ;
#14580=DIRECTION ( 'NONE',  ( -0.6830127018922180770, -0.6830127018922204085, -0.2588190451025213501 ) ) ;
#14582=EDGE_LOOP ( 'NONE', ( #132986, #134344, #84140, #24506, #117202, #56825, #140975, #138544, #100601, #105520, #41571, #53147, #115803, #141978, #89867, #61818, #15295, #131992, #105543, #55071, #60578, #23722, #21829, #8018, #125584, #123313, #13919, #3027, #102496, #109837, #119298, #112820, #126662, #97785, #42999, #64224, #136658, #25792, #45175, #82177, #10278, #101342, #34891, #110289, #102920, #133976, #25162, #98541, #91003, #118809, #34293, #103337, #75573, #67899, #92800, #9832, #4509, #93407, #28082, #27841, #20985, #75449, #55418, #73513, #138828, #79026, #125552, #32384, #78819, #88940, #141776, #139941, #1202, #5863, #25661, #121580, #136231, #78318, #130761, #90099, #76805, #89277, #118138, #11473, #65983, #84889, #129717, #107249, #115070, #89235, #74103, #111606, #49486, #109901, #72591, #38050, #19048, #111242, #51264, #118523, #74808, #23379, #123336, #93821, #1919 ) ) ;
#14584=DIRECTION ( 'NONE',  ( 0.3543493200069162685, -0.000000000000000000, -0.9351131265310288487 ) ) ;
#14585=( BOUNDED_CURVE ( )  B_SPLINE_CURVE ( 3, ( #46432, #67453, #88481, #79782 ),
 .UNSPECIFIED., .F., .T. ) 
 B_SPLINE_CURVE_WITH_KNOTS ( ( 4, 4 ),
 ( 1.208578181583238820, 1.359146454359468237 ),
 .UNSPECIFIED. ) 
 CURVE ( )  GEOMETRIC_REPRESENTATION_ITEM ( )  RATIONAL_B_SPLINE_CURVE ( ( 1.000000000000000000, 0.9981116584018945304, 0.9981116584018945304, 1.000000000000000000 ) ) 
 REPRESENTATION_ITEM ( '' )  );
#14586=DIRECTION ( 'NONE',  ( -0.7071067811865487940, 0.7071067811865463515, -0.000000000000000000 ) ) ;
#14587=EDGE_CURVE ( 'NONE', #98903, #6676, #22325, .T. ) ;
#14588=LINE ( 'NONE', #59549, #9527 ) ;
#14589=VECTOR ( 'NONE', #60583, 1000.000000000000000 ) ;
#14590=VERTEX_POINT ( 'NONE', #18221 ) ;
#14591=SURFACE_STYLE_USAGE ( .BOTH. , #92853 ) ;
#14592=VERTEX_POINT ( 'NONE', #131130 ) ;
#14593=PLANE ( 'NONE',  #16060 ) ;
#14594=VECTOR ( 'NONE', #125753, 1000.000000000000000 ) ;
#14595=LINE ( 'NONE', #93588, #94906 ) ;
#14596=DIRECTION ( 'NONE',  ( -0.6830127018922180770, -0.6830127018922204085, -0.2588190451025213501 ) ) ;
#14597=DIRECTION ( 'NONE',  ( -0.3543493200069162685, -0.000000000000000000, -0.9351131265310288487 ) ) ;
#14599=ORIENTED_EDGE ( 'NONE', *, *, #85632, .F. ) ;
#14600=DIRECTION ( 'NONE',  ( -0.6830127018922181881, 0.6830127018922202975, -0.2588190451025214056 ) ) ;
#14601=ADVANCED_FACE ( 'NONE', ( #117544 ), #62498, .F. ) ;
#14602=DIRECTION ( 'NONE',  ( -0.7071067811865486830, -0.7071067811865464625, 0.000000000000000000 ) ) ;
#14603=DIRECTION ( 'NONE',  ( 0.7071067811865487940, 0.7071067811865463515, -0.000000000000000000 ) ) ;
#14604=EDGE_LOOP ( 'NONE', ( #71627, #52128, #70863, #4227 ) ) ;
#14605=CARTESIAN_POINT ( 'NONE',  ( 36.48921356237310221, -27.52281430457080802, 5.000000000000000000 ) ) ;
#14607=LINE ( 'NONE', #112493, #26120 ) ;
#14608=ORIENTED_EDGE ( 'NONE', *, *, #8588, .F. ) ;
#14609=DIRECTION ( 'NONE',  ( 0.6830127018922180770, -0.6830127018922204085, -0.2588190451025213501 ) ) ;
#14610=ORIENTED_EDGE ( 'NONE', *, *, #11600, .F. ) ;
#14611=EDGE_CURVE ( 'NONE', #94430, #15705, #87620, .T. ) ;
#14612=ORIENTED_EDGE ( 'NONE', *, *, #100181, .F. ) ;
#14613=VECTOR ( 'NONE', #63719, 999.9999999999998863 ) ;
#14616=EDGE_LOOP ( 'NONE', ( #121587, #57220, #44910 ) ) ;
#14618=EDGE_CURVE ( 'NONE', #131061, #76695, #10740, .T. ) ;
#14619=LINE ( 'NONE', #78461, #69319 ) ;
#14620=ORIENTED_EDGE ( 'NONE', *, *, #41209, .F. ) ;
#14621=CARTESIAN_POINT ( 'NONE',  ( 5.207106781186507050, -8.240707523384198652, 5.000000000000000000 ) ) ;
#14622=CARTESIAN_POINT ( 'NONE',  ( 17.29298673570682254, -21.74070752338406720, 4.999753212805220670 ) ) ;
#14623=PLANE ( 'NONE',  #125438 ) ;
#14624=DIRECTION ( 'NONE',  ( -0.7071067811865486830, 0.7071067811865464625, 0.000000000000000000 ) ) ;
#14626=LINE ( 'NONE', #58906, #100302 ) ;
#14627=FACE_OUTER_BOUND ( 'NONE', #121326, .T. ) ;
#14628=DIRECTION ( 'NONE',  ( -0.7071067811865486830, 0.7071067811865464625, 0.000000000000000000 ) ) ;
#14629=EDGE_CURVE ( 'NONE', #37516, #31371, #32535, .T. ) ;
#14630=CARTESIAN_POINT ( 'NONE',  ( -60.29974487139158867, -27.71228299555248142, 4.000000000000000000 ) ) ;
#14632=VECTOR ( 'NONE', #58844, 1000.000000000000114 ) ;
#14633=EDGE_LOOP ( 'NONE', ( #113114, #86401, #34936, #24023 ) ) ;
#14634=VERTEX_POINT ( 'NONE', #86918 ) ;
#14636=EDGE_CURVE ( 'NONE', #14590, #9641, #66596, .T. ) ;
#14637=ORIENTED_EDGE ( 'NONE', *, *, #139102, .F. ) ;
#14638=ORIENTED_EDGE ( 'NONE', *, *, #136235, .T. ) ;
#14639=VERTEX_POINT ( 'NONE', #65182 ) ;
#14640=VECTOR ( 'NONE', #127746, 1000.000000000000000 ) ;
#14641=CARTESIAN_POINT ( 'NONE',  ( 19.05000000000000071, 3.174999999999997158, 5.000000000000000000 ) ) ;
#14643=PLANE ( 'NONE',  #23116 ) ;
#14644=ORIENTED_EDGE ( 'NONE', *, *, #41566, .T. ) ;
#14646=DIRECTION ( 'NONE',  ( -0.7071067811865486830, -0.7071067811865464625, 0.000000000000000000 ) ) ;
#14647=CARTESIAN_POINT ( 'NONE',  ( 34.92499999999998295, -17.33753812416080464, 4.000000000000000000 ) ) ;
#14648=CARTESIAN_POINT ( 'NONE',  ( 33.18398860626899705, 28.73617430169810305, 5.000000000000000000 ) ) ;
#14651=EDGE_CURVE ( 'NONE', #22333, #102502, #40053, .T. ) ;
#14652=DIRECTION ( 'NONE',  ( 0.6830127018922180770, -0.6830127018922204085, -0.2588190451025213501 ) ) ;
#14653=CARTESIAN_POINT ( 'NONE',  ( 29.99999999999979394, 17.96639925780207747, 5.000000000000000000 ) ) ;
#14654=CARTESIAN_POINT ( 'NONE',  ( 45.48921356237309510, -27.52281430457087197, 5.000000000000000000 ) ) ;
#14655=LINE ( 'NONE', #13911, #54943 ) ;
#14656=DIRECTION ( 'NONE',  ( 0.7071067811865486830, -0.7071067811865464625, -0.000000000000000000 ) ) ;
#14660=DIRECTION ( 'NONE',  ( 0.7071067811865486830, -0.7071067811865464625, -0.000000000000000000 ) ) ;
#14661=VECTOR ( 'NONE', #10325, 1000.000000000000000 ) ;
#14663=ORIENTED_EDGE ( 'NONE', *, *, #116922, .F. ) ;
#14664=ORIENTED_EDGE ( 'NONE', *, *, #40412, .F. ) ;
#14669=DIRECTION ( 'NONE',  ( -0.6830127018922181881, 0.6830127018922202975, -0.2588190451025214056 ) ) ;
#14670=CARTESIAN_POINT ( 'NONE',  ( -32.99451991528749062, 28.92564299267960948, 4.000000000000000000 ) ) ;
#14671=ORIENTED_EDGE ( 'NONE', *, *, #69941, .T. ) ;
#14673=VECTOR ( 'NONE', #25798, 1000.000000000000000 ) ;
#14674=DIRECTION ( 'NONE',  ( 1.000000000000000000, 0.000000000000000000, 0.000000000000000000 ) ) ;
#14675=CARTESIAN_POINT ( 'NONE',  ( -13.88982677111779296, -22.22500000000000497, 4.785647885939354751 ) ) ;
#14677=AXIS2_PLACEMENT_3D ( 'NONE', #89466, #23495, #3161 ) ;
#14679=DIRECTION ( 'NONE',  ( 0.7071067811865487940, -0.7071067811865463515, 0.000000000000000000 ) ) ;
#14680=EDGE_LOOP ( 'NONE', ( #88582, #66648, #101418, #40806 ) ) ;
#14682=DIRECTION ( 'NONE',  ( -0.000000000000000000, 0.3543493200069153248, 0.9351131265310292928 ) ) ;
#14687=ORIENTED_EDGE ( 'NONE', *, *, #139934, .F. ) ;
#14688=PLANE ( 'NONE',  #139683 ) ;
#14689=CARTESIAN_POINT ( 'NONE',  ( -29.99999999999978328, -15.03360074219758857, 5.000000000000000000 ) ) ;
#14690=CARTESIAN_POINT ( 'NONE',  ( -2.994519915287485734, 28.92564299267940342, 4.000000000000000000 ) ) ;
#14691=VECTOR ( 'NONE', #138111, 1000.000000000000000 ) ;
#14692=ADVANCED_FACE ( 'NONE', ( #33288 ), #128464, .T. ) ;
#14695=EDGE_CURVE ( 'NONE', #136110, #84461, #20917, .T. ) ;
#14698=ADVANCED_FACE ( 'NONE', ( #53577 ), #120951, .T. ) ;
#14699=ORIENTED_EDGE ( 'NONE', *, *, #222, .F. ) ;
#14701=CARTESIAN_POINT ( 'NONE',  ( -27.32816939922333432, -9.740707523384180888, 4.000000000000000000 ) ) ;
#14702=ORIENTED_EDGE ( 'NONE', *, *, #108832, .T. ) ;
#14703=ADVANCED_FACE ( 'NONE', ( #105955 ), #65906, .T. ) ;
#14706=FACE_OUTER_BOUND ( 'NONE', #114473, .T. ) ;
#14707=VECTOR ( 'NONE', #111963, 1000.000000000000227 ) ;
#14709=EDGE_CURVE ( 'NONE', #68652, #139204, #44130, .T. ) ;
#14710=FACE_BOUND ( 'NONE', #28499, .T. ) ;
#14711=EDGE_CURVE ( 'NONE', #44187, #91404, #97780, .T. ) ;
#14713=DIRECTION ( 'NONE',  ( -0.7071067811865486830, -0.7071067811865464625, 0.000000000000000000 ) ) ;
#14714=DIRECTION ( 'NONE',  ( -0.6830127018922181881, 0.6830127018922202975, -0.2588190451025214056 ) ) ;
#14715=VECTOR ( 'NONE', #72859, 999.9999999999998863 ) ;
#14716=DIRECTION ( 'NONE',  ( 0.6830127018922180770, -0.6830127018922204085, -0.2588190451025213501 ) ) ;
#14717=LINE ( 'NONE', #78558, #27269 ) ;
#14718=VERTEX_POINT ( 'NONE', #77489 ) ;
#14721=ORIENTED_EDGE ( 'NONE', *, *, #57904, .T. ) ;
#14722=ORIENTED_EDGE ( 'NONE', *, *, #8112, .T. ) ;
#14726=DIRECTION ( 'NONE',  ( 0.3543493200069162685, -0.000000000000000000, -0.9351131265310288487 ) ) ;
#14727=ORIENTED_EDGE ( 'NONE', *, *, #60055, .T. ) ;
#14728=CARTESIAN_POINT ( 'NONE',  ( 47.99451991528749062, 28.92564299267971251, 4.000000000000000000 ) ) ;
#14729=EDGE_CURVE ( 'NONE', #88325, #117852, #68067, .T. ) ;
#14731=CARTESIAN_POINT ( 'NONE',  ( 28.49999999999981171, -2.947814304570794075, 5.000000000000000000 ) ) ;
#14734=CARTESIAN_POINT ( 'NONE',  ( 21.75860074219781382, 21.72500000000000142, 5.000000000000000000 ) ) ;
#14735=LINE ( 'NONE', #3806, #12235 ) ;
#14736=CARTESIAN_POINT ( 'NONE',  ( 33.29974487139158867, -27.71228299555229313, 4.000000000000000000 ) ) ;
#14738=EDGE_CURVE ( 'NONE', #46867, #45528, #69464, .T. ) ;
#14739=ORIENTED_EDGE ( 'NONE', *, *, #10382, .F. ) ;
#14741=LINE ( 'NONE', #59018, #11927 ) ;
#14742=ORIENTED_EDGE ( 'NONE', *, *, #89505, .F. ) ;
#14743=ORIENTED_EDGE ( 'NONE', *, *, #46676, .F. ) ;
#14744=ORIENTED_EDGE ( 'NONE', *, *, #81342, .F. ) ;
#14745=CARTESIAN_POINT ( 'NONE',  ( 36.18398860626899705, 28.73617430169812437, 5.000000000000000000 ) ) ;
#14746=ORIENTED_EDGE ( 'NONE', *, *, #100350, .T. ) ;
#14748=VECTOR ( 'NONE', #18999, 1000.000000000000000 ) ;
#14750=DIRECTION ( 'NONE',  ( -0.7071067811865486830, -0.7071067811865464625, -0.000000000000000000 ) ) ;
#14751=VECTOR ( 'NONE', #45690, 1000.000000000000000 ) ;
#14753=CARTESIAN_POINT ( 'NONE',  ( 34.92499999999998295, -0.2815095627957336921, 4.759050581649326261 ) ) ;
#14755=DIRECTION ( 'NONE',  ( -0.6830127018922181881, 0.6830127018922202975, -0.2588190451025214056 ) ) ;
#14756=DIRECTION ( 'NONE',  ( -0.7071067811865486830, -0.7071067811865464625, -0.000000000000000000 ) ) ;
#14757=ADVANCED_FACE ( 'NONE', ( #91224 ), #24496, .F. ) ;
#14760=VERTEX_POINT ( 'NONE', #58627 ) ;
#14761=ORIENTED_EDGE ( 'NONE', *, *, #137874, .F. ) ;
#14762=LINE ( 'NONE', #59039, #137635 ) ;
#14763=CARTESIAN_POINT ( 'NONE',  ( 0.000000000000000000, -6.108550654416962544, -3.114665004254967950 ) ) ;
#14764=VECTOR ( 'NONE', #86460, 1000.000000000000000 ) ;
#14766=EDGE_LOOP ( 'NONE', ( #127644, #78010, #96208, #42375 ) ) ;
#14767=LINE ( 'NONE', #73968, #85307 ) ;
#14768=EDGE_CURVE ( 'NONE', #121120, #128690, #102799, .T. ) ;
#14770=PLANE ( 'NONE',  #83586 ) ;
#14771=DIRECTION ( 'NONE',  ( -0.7071067811865486830, 0.7071067811865464625, 0.000000000000000000 ) ) ;
#14772=VERTEX_POINT ( 'NONE', #125247 ) ;
#14773=LINE ( 'NONE', #112659, #99393 ) ;
#14774=CARTESIAN_POINT ( 'NONE',  ( -34.92500000000001137, 22.22500000000000142, 4.500000000000000888 ) ) ;
#14775=CARTESIAN_POINT ( 'NONE',  ( -11.20710678118646619, 0.7592924766157138627, 5.000000000000000000 ) ) ;
#14776=VECTOR ( 'NONE', #95181, 1000.000000000000000 ) ;
#14777=LINE ( 'NONE', #89479, #7721 ) ;
#14779=ORIENTED_EDGE ( 'NONE', *, *, #8270, .F. ) ;
#14780=EDGE_CURVE ( 'NONE', #103353, #60630, #2741, .T. ) ;
#14781=ORIENTED_EDGE ( 'NONE', *, *, #122242, .F. ) ;
#14783=VECTOR ( 'NONE', #26566, 1000.000000000000000 ) ;
#14785=VECTOR ( 'NONE', #36485, 1000.000000000000000 ) ;
#14788=CARTESIAN_POINT ( 'NONE',  ( 27.29974487139158512, -27.71228299555225405, 4.000000000000000000 ) ) ;
#14789=CARTESIAN_POINT ( 'NONE',  ( -30.18398860626900060, 28.73617430169808173, 5.000000000000000000 ) ) ;
#14790=CARTESIAN_POINT ( 'NONE',  ( 47.99451991528749062, 28.92564299267971251, 4.000000000000000000 ) ) ;
#14791=VERTEX_POINT ( 'NONE', #100652 ) ;
#14792=DIRECTION ( 'NONE',  ( -0.7071067811865486830, 0.7071067811865463515, 0.000000000000000000 ) ) ;
#14793=DIRECTION ( 'NONE',  ( -0.7071067811865486830, -0.7071067811865464625, 0.000000000000000000 ) ) ;
#14794=VECTOR ( 'NONE', #125175, 1000.000000000000000 ) ;
#14795=FACE_OUTER_BOUND ( 'NONE', #119232, .T. ) ;
#14797=LINE ( 'NONE', #59071, #9358 ) ;
#14798=DIRECTION ( 'NONE',  ( -0.000000000000000000, 0.000000000000000000, 1.000000000000000000 ) ) ;
#14800=ORIENTED_EDGE ( 'NONE', *, *, #143025, .F. ) ;
#14802=VERTEX_POINT ( 'NONE', #136829 ) ;
#14806=CARTESIAN_POINT ( 'NONE',  ( -48.18398860626899705, 28.73617430169820608, 5.000000000000000000 ) ) ;
#14807=CARTESIAN_POINT ( 'NONE',  ( 2.292893218813435219, 11.25929247661560773, 5.000000000000000000 ) ) ;
#14808=EDGE_CURVE ( 'NONE', #137770, #53831, #13601, .T. ) ;
#14809=DIRECTION ( 'NONE',  ( 0.6830127018922181881, 0.6830127018922202975, -0.2588190451025214056 ) ) ;
#14811=VERTEX_POINT ( 'NONE', #90481 ) ;
#14812=EDGE_CURVE ( 'NONE', #15122, #110128, #56474, .T. ) ;
#14814=LINE ( 'NONE', #90976, #125091 ) ;
#14815=LINE ( 'NONE', #35894, #109328 ) ;
#14816=DIRECTION ( 'NONE',  ( -1.000000000000000000, 0.000000000000000000, 0.000000000000000000 ) ) ;
#14819=VECTOR ( 'NONE', #62557, 1000.000000000000227 ) ;
#14821=ORIENTED_EDGE ( 'NONE', *, *, #74053, .F. ) ;
#14823=LINE ( 'NONE', #59095, #51656 ) ;
#14824=CARTESIAN_POINT ( 'NONE',  ( -15.00548008471250228, 28.92564299267927552, 4.000000000000000000 ) ) ;
#14825=DIRECTION ( 'NONE',  ( 2.781805975412905274E-17, -0.3543493200069152138, 0.9351131265310292928 ) ) ;
#14827=ADVANCED_FACE ( 'NONE', ( #135435 ), #47729, .F. ) ;
#14828=AXIS2_PLACEMENT_3D ( 'NONE', #128498, #5251, #105297 ) ;
#14829=CARTESIAN_POINT ( 'NONE',  ( 39.48921356237310221, -27.52281430457082934, 5.000000000000000000 ) ) ;
#14832=CARTESIAN_POINT ( 'NONE',  ( 20.70025512860841133, -27.71228299555191654, 4.000000000000000000 ) ) ;
#14833=VERTEX_POINT ( 'NONE', #36802 ) ;
#14834=EDGE_LOOP ( 'NONE', ( #20923, #97916, #95663, #130014 ) ) ;
#14836=LINE ( 'NONE', #59111, #126240 ) ;
#14837=PLANE ( 'NONE',  #88355 ) ;
#14838=CARTESIAN_POINT ( 'NONE',  ( 16.49999999999988987, -8.947814304570730570, 5.000000000000000000 ) ) ;
#14840=DIRECTION ( 'NONE',  ( -0.3543493200069162685, -0.000000000000000000, -0.9351131265310288487 ) ) ;
#14842=FACE_OUTER_BOUND ( 'NONE', #101970, .T. ) ;
#14843=CARTESIAN_POINT ( 'NONE',  ( -34.92500000000001137, 21.72500000000000142, 5.000000000000000000 ) ) ;
#14845=AXIS2_PLACEMENT_3D ( 'NONE', #43276, #65773, #54869 ) ;
#14846=DIRECTION ( 'NONE',  ( -0.000000000000000000, 0.3543493200069153248, 0.9351131265310292928 ) ) ;
#14847=ORIENTED_EDGE ( 'NONE', *, *, #18719, .F. ) ;
#14850=EDGE_LOOP ( 'NONE', ( #52008, #41064, #35573, #102886 ) ) ;
#14851=DIRECTION ( 'NONE',  ( 0.000000000000000000, 1.000000000000000000, 0.000000000000000000 ) ) ;
#14852=EDGE_CURVE ( 'NONE', #48269, #673, #1298, .T. ) ;
#14853=CARTESIAN_POINT ( 'NONE',  ( 30.47336096364196223, -5.240707523384228850, 16.25846745537502969 ) ) ;
#14854=DIRECTION ( 'NONE',  ( 0.7071067811865487940, -0.7071067811865463515, 0.000000000000000000 ) ) ;
#14855=CARTESIAN_POINT ( 'NONE',  ( -54.29974487139159578, -27.71228299555243879, 4.000000000000000000 ) ) ;
#14856=ORIENTED_EDGE ( 'NONE', *, *, #103078, .F. ) ;
#14857=VERTEX_POINT ( 'NONE', #81779 ) ;
#14858=CARTESIAN_POINT ( 'NONE',  ( -12.29974487139158512, -27.71228299555214747, 4.000000000000000000 ) ) ;
#14859=DIRECTION ( 'NONE',  ( 0.7071067811865486830, -0.7071067811865464625, -0.000000000000000000 ) ) ;
#14860=EDGE_CURVE ( 'NONE', #91475, #51456, #45582, .T. ) ;
#14861=EDGE_CURVE ( 'NONE', #128057, #32169, #23799, .T. ) ;
#14862=VERTEX_POINT ( 'NONE', #112241 ) ;
#14863=VECTOR ( 'NONE', #121036, 1000.000000000000000 ) ;
#14864=CARTESIAN_POINT ( 'NONE',  ( -4.019877749285451607, -17.24070752338410273, 20.23474786156468497 ) ) ;
#14865=ORIENTED_EDGE ( 'NONE', *, *, #95070, .F. ) ;
#14866=DIRECTION ( 'NONE',  ( 1.000000000000000000, 0.000000000000000000, 0.000000000000000000 ) ) ;
#14867=PLANE ( 'NONE',  #139743 ) ;
#14869=ORIENTED_EDGE ( 'NONE', *, *, #130400, .F. ) ;
#14871=VECTOR ( 'NONE', #25447, 1000.000000000000000 ) ;
#14872=FACE_BOUND ( 'NONE', #46012, .T. ) ;
#14873=EDGE_CURVE ( 'NONE', #110076, #59821, #95462, .T. ) ;
#14874=DIRECTION ( 'NONE',  ( -0.7071067811865486830, 0.7071067811865464625, 0.000000000000000000 ) ) ;
#14875=DIRECTION ( 'NONE',  ( 0.6830127018922180770, -0.6830127018922204085, -0.2588190451025213501 ) ) ;
#14876=DIRECTION ( 'NONE',  ( 0.7071067811865487940, 0.7071067811865463515, 0.000000000000000000 ) ) ;
#14877=LINE ( 'NONE', #135946, #17930 ) ;
#14878=AXIS2_PLACEMENT_3D ( 'NONE', #97856, #30460, #31182 ) ;
#14880=ORIENTED_EDGE ( 'NONE', *, *, #106291, .T. ) ;
#14884=ORIENTED_EDGE ( 'NONE', *, *, #115141, .T. ) ;
#14885=EDGE_CURVE ( 'NONE', #66262, #20118, #62144, .T. ) ;
#14886=CARTESIAN_POINT ( 'NONE',  ( -51.48921356237309510, -27.52281430457091460, 5.000000000000000000 ) ) ;
#14887=CARTESIAN_POINT ( 'NONE',  ( -57.29974487139158157, -27.71228299555246011, 4.000000000000000000 ) ) ;
#14889=CARTESIAN_POINT ( 'NONE',  ( -19.49999999999986500, -13.53360074219760101, 5.000000000000000000 ) ) ;
#14890=CARTESIAN_POINT ( 'NONE',  ( -9.328169399223465774, 8.259292476615632594, 4.000000000000000000 ) ) ;
#14891=ORIENTED_EDGE ( 'NONE', *, *, #131385, .T. ) ;
#14892=DIRECTION ( 'NONE',  ( 0.000000000000000000, 0.000000000000000000, 1.000000000000000000 ) ) ;
#14895=CARTESIAN_POINT ( 'NONE',  ( 1.589909354801671171, 9.759292476615625489, 11.28811694763778917 ) ) ;
#14896=EDGE_CURVE ( 'NONE', #95968, #78911, #27337, .T. ) ;
#14897=CARTESIAN_POINT ( 'NONE',  ( 28.49999999999980460, 4.466399257802221356, 5.000000000000000000 ) ) ;
#14899=LINE ( 'NONE', #28665, #19502 ) ;
#14900=CARTESIAN_POINT ( 'NONE',  ( 18.18398860626898994, 28.73617430169800002, 5.000000000000000000 ) ) ;
#14901=ORIENTED_EDGE ( 'NONE', *, *, #101781, .T. ) ;
#14902=VERTEX_POINT ( 'NONE', #140399 ) ;
#14903=VERTEX_POINT ( 'NONE', #128117 ) ;
#14904=EDGE_CURVE ( 'NONE', #31251, #74191, #104915, .T. ) ;
#14906=EDGE_CURVE ( 'NONE', #94849, #96996, #125975, .T. ) ;
#14908=EDGE_CURVE ( 'NONE', #134689, #141054, #128804, .T. ) ;
#14910=VERTEX_POINT ( 'NONE', #72343 ) ;
#14911=DIRECTION ( 'NONE',  ( 0.7071067811865486830, -0.7071067811865464625, -0.000000000000000000 ) ) ;
#14913=DIRECTION ( 'NONE',  ( -0.7071067811865486830, -0.7071067811865464625, 0.000000000000000000 ) ) ;
#14914=CARTESIAN_POINT ( 'NONE',  ( 34.92499999999998295, -3.281509562795708934, 4.759050581649326261 ) ) ;
#14915=FACE_OUTER_BOUND ( 'NONE', #75733, .T. ) ;
#14916=ORIENTED_EDGE ( 'NONE', *, *, #95497, .F. ) ;
#14917=EDGE_LOOP ( 'NONE', ( #84322, #126542, #26760, #100109 ) ) ;
#14919=DIRECTION ( 'NONE',  ( -0.7071067811865486830, -0.7071067811865464625, -0.000000000000000000 ) ) ;
#14920=PLANE ( 'NONE',  #39132 ) ;
#14922=ORIENTED_EDGE ( 'NONE', *, *, #122586, .F. ) ;
#14923=FACE_OUTER_BOUND ( 'NONE', #19536, .T. ) ;
#14924=ORIENTED_EDGE ( 'NONE', *, *, #107260, .F. ) ;
#14925=ORIENTED_EDGE ( 'NONE', *, *, #4452, .F. ) ;
#14926=ORIENTED_EDGE ( 'NONE', *, *, #24125, .F. ) ;
#14929=FACE_OUTER_BOUND ( 'NONE', #138940, .T. ) ;
#14930=CARTESIAN_POINT ( 'NONE',  ( -0.3281693992235289459, 11.25929247661561305, 4.000000000000000000 ) ) ;
#14931=LINE ( 'NONE', #101233, #115700 ) ;
#14932=CARTESIAN_POINT ( 'NONE',  ( -11.99999999999990585, -8.151047557385080466, -8.977947279169770312 ) ) ;
#14933=ORIENTED_EDGE ( 'NONE', *, *, #58807, .F. ) ;
#14935=DIRECTION ( 'NONE',  ( -0.000000000000000000, 0.000000000000000000, 1.000000000000000000 ) ) ;
#14938=LINE ( 'NONE', #90368, #136538 ) ;
#14939=CARTESIAN_POINT ( 'NONE',  ( 11.99999999999991296, -12.03360074219761700, 5.000000000000000000 ) ) ;
#14940=ORIENTED_EDGE ( 'NONE', *, *, #29800, .F. ) ;
#14941=AXIS2_PLACEMENT_3D ( 'NONE', #51028, #6041, #105385 ) ;
#14942=ORIENTED_EDGE ( 'NONE', *, *, #42892, .T. ) ;
#14943=EDGE_CURVE ( 'NONE', #90863, #82492, #117891, .T. ) ;
#14944=EDGE_LOOP ( 'NONE', ( #56018, #119212, #80529, #85160 ) ) ;
#14946=DIRECTION ( 'NONE',  ( -0.7071067811865486830, -0.7071067811865464625, -0.000000000000000000 ) ) ;
#14948=DIRECTION ( 'NONE',  ( -0.7071067811865486830, -0.7071067811865464625, -0.000000000000000000 ) ) ;
#14950=CARTESIAN_POINT ( 'NONE',  ( -14.67183060077637080, -12.74070752338415602, 4.000000000000000000 ) ) ;
#14951=FACE_OUTER_BOUND ( 'NONE', #128698, .T. ) ;
#14952=DIRECTION ( 'NONE',  ( 0.7071067811865487940, 0.7071067811865463515, 0.000000000000000000 ) ) ;
#14953=VECTOR ( 'NONE', #85205, 1000.000000000000114 ) ;
#14954=DIRECTION ( 'NONE',  ( 0.3543493200069163240, -0.000000000000000000, 0.9351131265310288487 ) ) ;
#14956=CARTESIAN_POINT ( 'NONE',  ( -27.12147316337130221, -20.24070752338407075, 7.412974875817854858 ) ) ;
#14957=VERTEX_POINT ( 'NONE', #71590 ) ;
#14959=EDGE_LOOP ( 'NONE', ( #16524, #136120, #116740, #142683 ) ) ;
#14960=LINE ( 'NONE', #81700, #2011 ) ;
#14961=CARTESIAN_POINT ( 'NONE',  ( -1.499999999999984013, 3.052185695429136647, 5.000000000000000000 ) ) ;
#14962=ORIENTED_EDGE ( 'NONE', *, *, #15351, .F. ) ;
#14963=EDGE_CURVE ( 'NONE', #19198, #133116, #17199, .T. ) ;
#14967=EDGE_CURVE ( 'NONE', #73784, #106314, #15714, .T. ) ;
#14968=CARTESIAN_POINT ( 'NONE',  ( 45.48921356237309510, -27.52281430457087197, 5.000000000000000000 ) ) ;
#14970=DIRECTION ( 'NONE',  ( 0.7071067811865486830, -0.7071067811865464625, -0.000000000000000000 ) ) ;
#14971=ORIENTED_EDGE ( 'NONE', *, *, #104059, .F. ) ;
#14972=DIRECTION ( 'NONE',  ( -0.7071067811865486830, -0.7071067811865464625, 0.000000000000000000 ) ) ;
#14975=DIRECTION ( 'NONE',  ( -0.7071067811865487940, 0.7071067811865463515, 0.000000000000000000 ) ) ;
#14976=AXIS2_PLACEMENT_3D ( 'NONE', #89305, #22575, #112484 ) ;
#14977=AXIS2_PLACEMENT_3D ( 'NONE', #76499, #21389, #61534 ) ;
#14978=CARTESIAN_POINT ( 'NONE',  ( 63.18398860626900415, 28.73617430169831621, 5.000000000000000000 ) ) ;
#14979=ORIENTED_EDGE ( 'NONE', *, *, #65120, .F. ) ;
#14980=VECTOR ( 'NONE', #54330, 1000.000000000000000 ) ;
#14981=EDGE_CURVE ( 'NONE', #61902, #34556, #94029, .T. ) ;
#14982=CARTESIAN_POINT ( 'NONE',  ( -23.99999999999982592, -22.06887692260758982, 4.000000000000000000 ) ) ;
#14983=CARTESIAN_POINT ( 'NONE',  ( 2.510786437626908008, -27.52281430457053446, 5.000000000000000000 ) ) ;
#14984=CARTESIAN_POINT ( 'NONE',  ( 20.20710678118641113, -8.240707523384191546, 5.000000000000000000 ) ) ;
#14986=CARTESIAN_POINT ( 'NONE',  ( -9.489213562373095101, -27.52281430457062328, 5.000000000000000000 ) ) ;
#14987=DIRECTION ( 'NONE',  ( 0.7071067811865486830, -0.7071067811865464625, -0.000000000000000000 ) ) ;
#14988=PLANE ( 'NONE',  #43264 ) ;
#14990=EDGE_CURVE ( 'NONE', #65015, #3074, #38952, .T. ) ;
#14991=DIRECTION ( 'NONE',  ( -0.7071067811865486830, -0.7071067811865464625, 0.000000000000000000 ) ) ;
#14992=ORIENTED_EDGE ( 'NONE', *, *, #116380, .F. ) ;
#14994=LINE ( 'NONE', #61423, #33877 ) ;
#14995=FACE_OUTER_BOUND ( 'NONE', #69529, .T. ) ;
#14996=FACE_OUTER_BOUND ( 'NONE', #140776, .T. ) ;
#14997=EDGE_LOOP ( 'NONE', ( #120596, #131543, #107022 ) ) ;
#14998=EDGE_CURVE ( 'NONE', #13363, #86911, #117194, .T. ) ;
#15000=CARTESIAN_POINT ( 'NONE',  ( 8.510786437626906675, -27.52281430457049183, 5.000000000000000000 ) ) ;
#15001=ORIENTED_EDGE ( 'NONE', *, *, #121744, .T. ) ;
#15002=CARTESIAN_POINT ( 'NONE',  ( -10.49999999999992895, -2.173586137069142499, -4.605770156576136642 ) ) ;
#15003=PLANE ( 'NONE',  #7735 ) ;
#15005=EDGE_LOOP ( 'NONE', ( #61823, #103645, #46896 ) ) ;
#15006=CARTESIAN_POINT ( 'NONE',  ( 29.99999999999979039, 20.70535890316563865, 1.956823837851847214 ) ) ;
#15007=EDGE_CURVE ( 'NONE', #104985, #45577, #6984, .T. ) ;
#15009=DIRECTION ( 'NONE',  ( -0.7071067811865486830, -0.7071067811865464625, -0.000000000000000000 ) ) ;
#15011=ORIENTED_EDGE ( 'NONE', *, *, #112706, .T. ) ;
#15012=ORIENTED_EDGE ( 'NONE', *, *, #113395, .F. ) ;
#15013=ORIENTED_EDGE ( 'NONE', *, *, #67381, .T. ) ;
#15016=CYLINDRICAL_SURFACE ( 'NONE', #123851, 0.5000000000000004441 ) ;
#15017=EDGE_CURVE ( 'NONE', #105758, #100682, #137563, .T. ) ;
#15018=DIRECTION ( 'NONE',  ( -0.7071067811865486830, -0.7071067811865464625, -0.000000000000000000 ) ) ;
#15019=CARTESIAN_POINT ( 'NONE',  ( -18.18398860626898994, 28.73617430169800002, 5.000000000000000000 ) ) ;
#15020=DIRECTION ( 'NONE',  ( 0.7071067811865486830, -0.7071067811865464625, -0.000000000000000000 ) ) ;
#15021=ORIENTED_EDGE ( 'NONE', *, *, #84871, .F. ) ;
#15022=CARTESIAN_POINT ( 'NONE',  ( 0.000000000000000000, 0.000000000000000000, 5.000000000000000000 ) ) ;
#15023=DIRECTION ( 'NONE',  ( -0.7071067811865486830, -0.7071067811865464625, 0.000000000000000000 ) ) ;
#15024=EDGE_CURVE ( 'NONE', #106541, #47360, #17872, .T. ) ;
#15027=ORIENTED_EDGE ( 'NONE', *, *, #51417, .F. ) ;
#15028=CARTESIAN_POINT ( 'NONE',  ( -25.49999999999982947, 22.22500000000000853, 4.362957392718830540 ) ) ;
#15030=CARTESIAN_POINT ( 'NONE',  ( 51.18398860626899705, 28.73617430169823095, 5.000000000000000000 ) ) ;
#15032=EDGE_LOOP ( 'NONE', ( #63072, #69489, #55944, #59862 ) ) ;
#15033=EDGE_LOOP ( 'NONE', ( #141267, #131669, #9013, #77609 ) ) ;
#15034=CARTESIAN_POINT ( 'NONE',  ( 24.71230993966010914, -21.73547319004781997, 4.999917730833664642 ) ) ;
#15035=EDGE_CURVE ( 'NONE', #128295, #76093, #9119, .T. ) ;
#15036=ADVANCED_FACE ( 'NONE', ( #54148 ), #65747, .F. ) ;
#15038=CARTESIAN_POINT ( 'NONE',  ( -15.51168605928422295, 6.759292476615645917, 16.35960578974473023 ) ) ;
#15040=CARTESIAN_POINT ( 'NONE',  ( 11.34328999833780394, 3.759292476615688550, 13.27625715073267898 ) ) ;
#15041=LINE ( 'NONE', #125251, #118366 ) ;
#15042=VECTOR ( 'NONE', #129478, 999.9999999999998863 ) ;
#15043=ORIENTED_EDGE ( 'NONE', *, *, #119802, .T. ) ;
#15044=ORIENTED_EDGE ( 'NONE', *, *, #73043, .T. ) ;
#15045=EDGE_CURVE ( 'NONE', #59700, #62370, #65009, .T. ) ;
#15047=DIRECTION ( 'NONE',  ( 0.7071067811865486830, -0.7071067811865464625, -0.000000000000000000 ) ) ;
#15048=VERTEX_POINT ( 'NONE', #131679 ) ;
#15049=EDGE_CURVE ( 'NONE', #17476, #118799, #10573, .T. ) ;
#15050=CARTESIAN_POINT ( 'NONE',  ( -7.499999999999944045, -10.53360074219763121, 5.000000000000000000 ) ) ;
#15052=VECTOR ( 'NONE', #100745, 1000.000000000000000 ) ;
#15053=DIRECTION ( 'NONE',  ( -0.7071067811865486830, 0.7071067811865464625, 0.000000000000000000 ) ) ;
#15054=PLANE ( 'NONE',  #142146 ) ;
#15055=DIRECTION ( 'NONE',  ( -0.6830127018922180770, -0.6830127018922204085, -0.2588190451025213501 ) ) ;
#15056=DIRECTION ( 'NONE',  ( 0.6830127018922180770, -0.6830127018922204085, -0.2588190451025213501 ) ) ;
#15057=ORIENTED_EDGE ( 'NONE', *, *, #56308, .F. ) ;
#15058=LINE ( 'NONE', #126675, #84228 ) ;
#15059=LINE ( 'NONE', #70914, #72002 ) ;
#15060=ORIENTED_EDGE ( 'NONE', *, *, #75996, .T. ) ;
#15061=CARTESIAN_POINT ( 'NONE',  ( -32.28769006033950006, -21.73547319004780576, 4.999917730833664642 ) ) ;
#15062=EDGE_LOOP ( 'NONE', ( #104055, #88309, #66520, #59457, #17516 ) ) ;
#15064=FACE_OUTER_BOUND ( 'NONE', #131516, .T. ) ;
#15065=VERTEX_POINT ( 'NONE', #42549 ) ;
#15066=EDGE_LOOP ( 'NONE', ( #48630, #24483, #89181, #137375 ) ) ;
#15067=CARTESIAN_POINT ( 'NONE',  ( -75.18398860626899705, 28.73617430169839793, 5.000000000000000000 ) ) ;
#15069=VECTOR ( 'NONE', #23185, 1000.000000000000000 ) ;
#15070=EDGE_CURVE ( 'NONE', #121941, #129287, #22166, .T. ) ;
#15071=DIRECTION ( 'NONE',  ( 0.7071067811865486830, -0.7071067811865464625, -0.000000000000000000 ) ) ;
#15072=AXIS2_PLACEMENT_3D ( 'NONE', #70767, #136696, #114914 ) ;
#15073=EDGE_CURVE ( 'NONE', #57955, #51470, #30950, .T. ) ;
#15074=AXIS2_PLACEMENT_3D ( 'NONE', #110643, #20802, #66480 ) ;
#15075=CARTESIAN_POINT ( 'NONE',  ( -15.48921356237309510, -27.52281430457066236, 5.000000000000000000 ) ) ;
#15080=DIRECTION ( 'NONE',  ( -0.3543493200069162685, -0.000000000000000000, -0.9351131265310288487 ) ) ;
#15081=CARTESIAN_POINT ( 'NONE',  ( -26.41358365631583993, -22.22500000000000142, 8.225293826072885395 ) ) ;
#15082=DIRECTION ( 'NONE',  ( 0.7071067811865487940, -0.7071067811865463515, 0.000000000000000000 ) ) ;
#15084=LINE ( 'NONE', #60058, #19652 ) ;
#15085=ORIENTED_EDGE ( 'NONE', *, *, #79005, .T. ) ;
#15086=DIRECTION ( 'NONE',  ( 0.3543493200069163240, -0.000000000000000000, 0.9351131265310288487 ) ) ;
#15087=FACE_OUTER_BOUND ( 'NONE', #127601, .T. ) ;
#15088=ORIENTED_EDGE ( 'NONE', *, *, #46116, .F. ) ;
#15091=ORIENTED_EDGE ( 'NONE', *, *, #38859, .F. ) ;
#15092=DIRECTION ( 'NONE',  ( -0.6830127018922181881, 0.6830127018922202975, -0.2588190451025214056 ) ) ;
#15093=CARTESIAN_POINT ( 'NONE',  ( -84.48921356237309510, -27.52281430457114197, 5.000000000000000000 ) ) ;
#15094=DIRECTION ( 'NONE',  ( -0.7071067811865487940, 0.7071067811865463515, -0.000000000000000000 ) ) ;
#15095=PLANE ( 'NONE',  #101985 ) ;
#15096=ORIENTED_EDGE ( 'NONE', *, *, #49554, .F. ) ;
#15097=DIRECTION ( 'NONE',  ( -0.3543493200069162685, -0.000000000000000000, -0.9351131265310288487 ) ) ;
#15099=DIRECTION ( 'NONE',  ( 0.7071067811865487940, 0.7071067811865463515, 0.000000000000000000 ) ) ;
#15103=VERTEX_POINT ( 'NONE', #32362 ) ;
#15104=VERTEX_POINT ( 'NONE', #132427 ) ;
#15105=ORIENTED_EDGE ( 'NONE', *, *, #138313, .F. ) ;
#15108=DIRECTION ( 'NONE',  ( -0.3543493200069163240, 0.000000000000000000, 0.9351131265310288487 ) ) ;
#15109=FACE_OUTER_BOUND ( 'NONE', #34531, .T. ) ;
#15110=VERTEX_POINT ( 'NONE', #30206 ) ;
#15112=DIRECTION ( 'NONE',  ( 1.000000000000000000, 0.000000000000000000, 0.000000000000000000 ) ) ;
#15113=CARTESIAN_POINT ( 'NONE',  ( 57.18398860626899705, 28.73617430169827358, 5.000000000000000000 ) ) ;
#15115=PLANE ( 'NONE',  #12105 ) ;
#15116=ORIENTED_EDGE ( 'NONE', *, *, #119010, .T. ) ;
#15117=CARTESIAN_POINT ( 'NONE',  ( -57.18398860626899705, 28.73617430169827358, 5.000000000000000000 ) ) ;
#15119=EDGE_CURVE ( 'NONE', #68468, #140795, #141097, .T. ) ;
#15121=ORIENTED_EDGE ( 'NONE', *, *, #50073, .T. ) ;
#15122=VERTEX_POINT ( 'NONE', #120033 ) ;
#15123=EDGE_CURVE ( 'NONE', #10977, #114516, #41809, .T. ) ;
#15124=ADVANCED_FACE ( 'NONE', ( #130261 ), #75180, .F. ) ;
#15125=LINE ( 'NONE', #121227, #104757 ) ;
#15126=CARTESIAN_POINT ( 'NONE',  ( -25.49999999999981881, 6.277155672890249782, -3.510561720658882834 ) ) ;
#15127=DIRECTION ( 'NONE',  ( 0.7071067811865487940, 0.7071067811865463515, 0.000000000000000000 ) ) ;
#15128=EDGE_LOOP ( 'NONE', ( #88686, #80502, #66759, #97087, #106301 ) ) ;
#15130=ORIENTED_EDGE ( 'NONE', *, *, #67320, .F. ) ;
#15132=EDGE_CURVE ( 'NONE', #44266, #129569, #85286, .T. ) ;
#15133=DIRECTION ( 'NONE',  ( 0.000000000000000000, -1.000000000000000000, 0.000000000000000000 ) ) ;
#15134=LINE ( 'NONE', #4210, #62433 ) ;
#15137=DIRECTION ( 'NONE',  ( 0.6830127018922181881, 0.6830127018922202975, -0.2588190451025214056 ) ) ;
#15138=LINE ( 'NONE', #2847, #113085 ) ;
#15139=VECTOR ( 'NONE', #1107, 1000.000000000000000 ) ;
#15140=ADVANCED_FACE ( 'NONE', ( #142561 ), #107753, .T. ) ;
#15141=CARTESIAN_POINT ( 'NONE',  ( 53.99451991528749062, 28.92564299267975869, 4.000000000000000000 ) ) ;
#15142=DIRECTION ( 'NONE',  ( -0.7071067811865487940, 0.7071067811865463515, -0.000000000000000000 ) ) ;
#15143=LINE ( 'NONE', #58001, #85355 ) ;
#15145=DIRECTION ( 'NONE',  ( 1.000000000000000000, 0.000000000000000000, 0.000000000000000000 ) ) ;
#15146=CARTESIAN_POINT ( 'NONE',  ( 0.7071067811865398012, -6.740707523384219968, 5.000000000000000000 ) ) ;
#15147=DIRECTION ( 'NONE',  ( -0.6830127018922181881, 0.6830127018922202975, -0.2588190451025214056 ) ) ;
#15148=CARTESIAN_POINT ( 'NONE',  ( -29.24139925780183091, 21.72500000000000853, 5.000000000000000000 ) ) ;
#15149=ORIENTED_EDGE ( 'NONE', *, *, #86582, .T. ) ;
#15150=ORIENTED_EDGE ( 'NONE', *, *, #28617, .T. ) ;
#15153=ADVANCED_FACE ( 'NONE', ( #25029 ), #59148, .F. ) ;
#15155=VECTOR ( 'NONE', #28744, 999.9999999999998863 ) ;
#15157=CARTESIAN_POINT ( 'NONE',  ( -10.49999999999992184, 22.01701374228154862, 2.453858888625655599 ) ) ;
#15159=CARTESIAN_POINT ( 'NONE',  ( -21.48921356237309155, -27.52281430457070499, 5.000000000000000000 ) ) ;
#15160=ORIENTED_EDGE ( 'NONE', *, *, #25989, .F. ) ;
#15161=EDGE_CURVE ( 'NONE', #116464, #124871, #89581, .T. ) ;
#15162=LINE ( 'NONE', #89190, #124997 ) ;
#15163=CARTESIAN_POINT ( 'NONE',  ( 0.000000000000000000, 0.000000000000000000, 5.000000000000000000 ) ) ;
#15164=CARTESIAN_POINT ( 'NONE',  ( 24.29974487139158867, -27.71228299555223273, 4.000000000000000000 ) ) ;
#15166=LINE ( 'NONE', #81921, #49402 ) ;
#15167=DIRECTION ( 'NONE',  ( -0.000000000000000000, 0.000000000000000000, 1.000000000000000000 ) ) ;
#15168=DIRECTION ( 'NONE',  ( -0.6830127018922180770, -0.6830127018922204085, -0.2588190451025213501 ) ) ;
#15169=EDGE_CURVE ( 'NONE', #108750, #129128, #36625, .T. ) ;
#15170=DIRECTION ( 'NONE',  ( 0.6830127018922181881, 0.6830127018922202975, -0.2588190451025214056 ) ) ;
#15171=CARTESIAN_POINT ( 'NONE',  ( 34.49999999999975131, 9.431123077392088661, 4.000000000000000000 ) ) ;
#15172=CARTESIAN_POINT ( 'NONE',  ( 34.45011844616452379, 9.002304141593850062, 4.999999999999999112 ) ) ;
#15173=CARTESIAN_POINT ( 'NONE',  ( -30.18398860626900060, 28.73617430169808173, 5.000000000000000000 ) ) ;
#15176=ORIENTED_EDGE ( 'NONE', *, *, #42565, .T. ) ;
#15177=EDGE_LOOP ( 'NONE', ( #7585, #25003, #24204, #12135 ) ) ;
#15178=AXIS2_PLACEMENT_3D ( 'NONE', #137710, #70347, #127526 ) ;
#15180=VERTEX_POINT ( 'NONE', #56994 ) ;
#15181=VECTOR ( 'NONE', #2792, 1000.000000000000000 ) ;
#15182=EDGE_CURVE ( 'NONE', #103350, #330, #35954, .T. ) ;
#15184=AXIS2_PLACEMENT_3D ( 'NONE', #42641, #86839, #77416 ) ;
#15185=DIRECTION ( 'NONE',  ( 0.7071067811865487940, 0.7071067811865463515, -0.000000000000000000 ) ) ;
#15186=ORIENTED_EDGE ( 'NONE', *, *, #131358, .T. ) ;
#15187=CARTESIAN_POINT ( 'NONE',  ( 0.000000000000000000, 0.000000000000000000, 5.000000000000000000 ) ) ;
#15189=ADVANCED_FACE ( 'NONE', ( #103300 ), #58447, .F. ) ;
#15192=ADVANCED_FACE ( 'NONE', ( #88904 ), #68577, .F. ) ;
#15194=LINE ( 'NONE', #15880, #112542 ) ;
#15195=DIRECTION ( 'NONE',  ( -0.6830127018922181881, 0.6830127018922202975, -0.2588190451025214056 ) ) ;
#15196=EDGE_CURVE ( 'NONE', #142313, #48699, #122194, .T. ) ;
#15197=ORIENTED_EDGE ( 'NONE', *, *, #114829, .T. ) ;
#15199=EDGE_LOOP ( 'NONE', ( #76837, #15837, #18483, #10609 ) ) ;
#15200=DIRECTION ( 'NONE',  ( -0.7071067811865487940, 0.7071067811865463515, 0.000000000000000000 ) ) ;
#15203=ORIENTED_EDGE ( 'NONE', *, *, #70044, .T. ) ;
#15204=ORIENTED_EDGE ( 'NONE', *, *, #57198, .F. ) ;
#15205=EDGE_CURVE ( 'NONE', #128869, #34223, #33802, .T. ) ;
#15206=DIRECTION ( 'NONE',  ( 0.7071067811865487940, 0.7071067811865463515, -0.000000000000000000 ) ) ;
#15207=ORIENTED_EDGE ( 'NONE', *, *, #102808, .F. ) ;
#15208=EDGE_LOOP ( 'NONE', ( #38756, #45143, #117362, #9382 ) ) ;
#15209=FACE_OUTER_BOUND ( 'NONE', #732, .T. ) ;
#15210=DIRECTION ( 'NONE',  ( 0.7071067811865486830, -0.7071067811865464625, -0.000000000000000000 ) ) ;
#15211=EDGE_LOOP ( 'NONE', ( #40459, #99159, #98147, #88160 ) ) ;
#15212=PLANE ( 'NONE',  #66818 ) ;
#15214=FACE_OUTER_BOUND ( 'NONE', #126886, .T. ) ;
#15216=ADVANCED_FACE ( 'NONE', ( #67134 ), #23614, .F. ) ;
#15217=FACE_BOUND ( 'NONE', #55286, .T. ) ;
#15218=VERTEX_POINT ( 'NONE', #100480 ) ;
#15219=DIRECTION ( 'NONE',  ( -0.000000000000000000, 0.3543493200069153248, 0.9351131265310292928 ) ) ;
#15221=DIRECTION ( 'NONE',  ( 0.7071067811865486830, -0.7071067811865464625, -0.000000000000000000 ) ) ;
#15224=ORIENTED_EDGE ( 'NONE', *, *, #8422, .T. ) ;
#15225=ORIENTED_EDGE ( 'NONE', *, *, #125237, .F. ) ;
#15226=ORIENTED_EDGE ( 'NONE', *, *, #10804, .F. ) ;
#15228=EDGE_CURVE ( 'NONE', #99670, #36919, #1128, .T. ) ;
#15230=ORIENTED_EDGE ( 'NONE', *, *, #85897, .F. ) ;
#15231=CARTESIAN_POINT ( 'NONE',  ( 7.499999999999951150, 8.319652575858395238, -8.582050562765809687 ) ) ;
#15233=DIRECTION ( 'NONE',  ( 0.6830127018922181881, 0.6830127018922202975, -0.2588190451025214056 ) ) ;
#15235=ORIENTED_EDGE ( 'NONE', *, *, #2526, .T. ) ;
#15236=LINE ( 'NONE', #36318, #125533 ) ;
#15238=DIRECTION ( 'NONE',  ( -0.7071067811865486830, -0.7071067811865464625, 0.000000000000000000 ) ) ;
#15239=ADVANCED_FACE ( 'NONE', ( #133812 ), #34498, .T. ) ;
#15240=DIRECTION ( 'NONE',  ( 1.000000000000000000, 0.000000000000000000, 0.000000000000000000 ) ) ;
#15241=CARTESIAN_POINT ( 'NONE',  ( 12.79289321881337038, -14.24070752338414003, 5.000000000000000000 ) ) ;
#15242=FACE_OUTER_BOUND ( 'NONE', #55535, .T. ) ;
#15243=DIRECTION ( 'NONE',  ( -0.7071067811865487940, 0.7071067811865463515, 0.000000000000000000 ) ) ;
#15244=EDGE_LOOP ( 'NONE', ( #13844, #112031, #89544, #102454 ) ) ;
#15245=EDGE_LOOP ( 'NONE', ( #11463, #44643, #137019, #8292 ) ) ;
#15246=ORIENTED_EDGE ( 'NONE', *, *, #68640, .T. ) ;
#15247=ORIENTED_EDGE ( 'NONE', *, *, #92296, .T. ) ;
#15248=EDGE_LOOP ( 'NONE', ( #130288, #105074, #48002, #21915 ) ) ;
#15249=ORIENTED_EDGE ( 'NONE', *, *, #112108, .F. ) ;
#15250=CARTESIAN_POINT ( 'NONE',  ( 45.48921356237309510, -27.52281430457087197, 5.000000000000000000 ) ) ;
#15251=EDGE_CURVE ( 'NONE', #54369, #7225, #67886, .T. ) ;
#15252=FACE_OUTER_BOUND ( 'NONE', #35552, .T. ) ;
#15253=VERTEX_POINT ( 'NONE', #102628 ) ;
#15256=CARTESIAN_POINT ( 'NONE',  ( -15.71757738642556568, -21.73023691814493219, 5.000000000000000000 ) ) ;
#15258=VECTOR ( 'NONE', #16992, 999.9999999999998863 ) ;
#15259=EDGE_LOOP ( 'NONE', ( #123639, #108229, #116736, #53927 ) ) ;
#15261=DIRECTION ( 'NONE',  ( -0.000000000000000000, -0.000000000000000000, 1.000000000000000000 ) ) ;
#15263=ORIENTED_EDGE ( 'NONE', *, *, #70212, .F. ) ;
#15265=DIRECTION ( 'NONE',  ( -0.6830127018922181881, 0.6830127018922202975, -0.2588190451025214056 ) ) ;
#15266=ORIENTED_EDGE ( 'NONE', *, *, #117510, .F. ) ;
#15267=CARTESIAN_POINT ( 'NONE',  ( -36.48921356237310221, -27.52281430457080802, 5.000000000000000000 ) ) ;
#15268=VECTOR ( 'NONE', #73310, 1000.000000000000000 ) ;
#15270=DIRECTION ( 'NONE',  ( 0.7071067811865487940, 0.7071067811865463515, 0.000000000000000000 ) ) ;
#15272=ORIENTED_EDGE ( 'NONE', *, *, #23042, .T. ) ;
#15273=CARTESIAN_POINT ( 'NONE',  ( 4.171830600776448961, 6.759292476615649470, 4.000000000000000000 ) ) ;
#15275=CARTESIAN_POINT ( 'NONE',  ( 23.99451991528749062, 28.92564299267954908, 4.000000000000000000 ) ) ;
#15276=DIRECTION ( 'NONE',  ( 1.000000000000000000, 0.000000000000000000, 0.000000000000000000 ) ) ;
#15277=VERTEX_POINT ( 'NONE', #46112 ) ;
#15278=CARTESIAN_POINT ( 'NONE',  ( 0.000000000000000000, 0.000000000000000000, 5.000000000000000000 ) ) ;
#15279=CARTESIAN_POINT ( 'NONE',  ( -33.29974487139158867, -27.71228299555229313, 4.000000000000000000 ) ) ;
#15281=PLANE ( 'NONE',  #141298 ) ;
#15282=VERTEX_POINT ( 'NONE', #112764 ) ;
#15283=ADVANCED_FACE ( 'NONE', ( #91047 ), #79485, .F. ) ;
#15284=ADVANCED_FACE ( 'NONE', ( #124360 ), #2552, .F. ) ;
#15285=EDGE_LOOP ( 'NONE', ( #24096, #17969, #24122, #137167 ) ) ;
#15286=CARTESIAN_POINT ( 'NONE',  ( -78.18398860626899705, 28.73617430169841924, 5.000000000000000000 ) ) ;
#15287=CARTESIAN_POINT ( 'NONE',  ( -18.70710678118640402, -3.740707523384248390, 5.000000000000000000 ) ) ;
#15289=PLANE ( 'NONE',  #92869 ) ;
#15290=EDGE_CURVE ( 'NONE', #22900, #73261, #24742, .T. ) ;
#15292=LINE ( 'NONE', #83455, #61474 ) ;
#15294=ADVANCED_FACE ( 'NONE', ( #3949 ), #105441, .T. ) ;
#15295=ORIENTED_EDGE ( 'NONE', *, *, #45204, .T. ) ;
#15296=DIRECTION ( 'NONE',  ( 0.7071067811865487940, 0.7071067811865463515, 0.000000000000000000 ) ) ;
#15297=CARTESIAN_POINT ( 'NONE',  ( 0.4892135623730947680, -27.52281430457055578, 5.000000000000000000 ) ) ;
#15298=ADVANCED_FACE ( 'NONE', ( #50378 ), #59833, .F. ) ;
#15299=DIRECTION ( 'NONE',  ( 0.7071067811865487940, -0.7071067811865463515, 0.000000000000000000 ) ) ;
#15300=FACE_OUTER_BOUND ( 'NONE', #25737, .T. ) ;
#15302=VECTOR ( 'NONE', #28758, 1000.000000000000000 ) ;
#15303=DIRECTION ( 'NONE',  ( 0.7071067811865487940, -0.7071067811865463515, 0.000000000000000000 ) ) ;
#15305=CARTESIAN_POINT ( 'NONE',  ( -34.92500000000001137, 4.800094516027155755, 4.759050581649336031 ) ) ;
#15306=LINE ( 'NONE', #126940, #128724 ) ;
#15307=ORIENTED_EDGE ( 'NONE', *, *, #106316, .F. ) ;
#15308=ORIENTED_EDGE ( 'NONE', *, *, #70247, .F. ) ;
#15309=VERTEX_POINT ( 'NONE', #117726 ) ;
#15311=ADVANCED_FACE ( 'NONE', ( #27899 ), #6813, .F. ) ;
#15312=VERTEX_POINT ( 'NONE', #73558 ) ;
#15313=ORIENTED_EDGE ( 'NONE', *, *, #31755, .F. ) ;
#15314=ORIENTED_EDGE ( 'NONE', *, *, #61087, .T. ) ;
#15316=PLANE ( 'NONE',  #57190 ) ;
#15317=CARTESIAN_POINT ( 'NONE',  ( -34.42500000000001137, -22.22500000000000142, 0.4999999999999995559 ) ) ;
#15318=VERTEX_POINT ( 'NONE', #17030 ) ;
#15319=DIRECTION ( 'NONE',  ( -0.000000000000000000, 0.000000000000000000, 1.000000000000000000 ) ) ;
#15320=ADVANCED_FACE ( 'NONE', ( #16270 ), #115574, .F. ) ;
#15321=LINE ( 'NONE', #58202, #11565 ) ;
#15322=CARTESIAN_POINT ( 'NONE',  ( -12.18398860626900060, 28.73617430169795739, 5.000000000000000000 ) ) ;
#15324=ORIENTED_EDGE ( 'NONE', *, *, #94215, .T. ) ;
#15325=CARTESIAN_POINT ( 'NONE',  ( -38.99451991528749062, 28.92564299267965211, 4.000000000000000000 ) ) ;
#15326=LINE ( 'NONE', #73336, #125697 ) ;
#15327=LINE ( 'NONE', #48019, #17141 ) ;
#15328=LINE ( 'NONE', #13194, #142270 ) ;
#15329=EDGE_CURVE ( 'NONE', #118822, #76747, #5405, .T. ) ;
#15330=DIRECTION ( 'NONE',  ( -0.7071067811865487940, 0.7071067811865463515, -0.000000000000000000 ) ) ;
#15331=DIRECTION ( 'NONE',  ( -0.7071067811865486830, -0.7071067811865464625, 0.000000000000000000 ) ) ;
#15334=CARTESIAN_POINT ( 'NONE',  ( 17.99451991528748351, 28.92564299267950645, 4.000000000000000000 ) ) ;
#15336=ORIENTED_EDGE ( 'NONE', *, *, #33676, .T. ) ;
#15337=VERTEX_POINT ( 'NONE', #60570 ) ;
#15340=VECTOR ( 'NONE', #6262, 999.9999999999998863 ) ;
#15342=LINE ( 'NONE', #138596, #41704 ) ;
#15343=DIRECTION ( 'NONE',  ( 0.7071067811865486830, -0.7071067811865464625, -0.000000000000000000 ) ) ;
#15344=ORIENTED_EDGE ( 'NONE', *, *, #110987, .T. ) ;
#15345=CARTESIAN_POINT ( 'NONE',  ( 17.51078643762690845, -27.52281430457043143, 5.000000000000000000 ) ) ;
#15346=CARTESIAN_POINT ( 'NONE',  ( 65.99451991528749772, 28.92564299267984396, 4.000000000000000000 ) ) ;
#15347=DIRECTION ( 'NONE',  ( -0.7071067811865486830, -0.7071067811865464625, 0.000000000000000000 ) ) ;
#15350=ORIENTED_EDGE ( 'NONE', *, *, #128077, .F. ) ;
#15351=EDGE_CURVE ( 'NONE', #52228, #103613, #26476, .T. ) ;
#15352=CARTESIAN_POINT ( 'NONE',  ( -42.29974487139158157, -27.71228299555235708, 4.000000000000000000 ) ) ;
#15353=ORIENTED_EDGE ( 'NONE', *, *, #50259, .F. ) ;
#15354=CARTESIAN_POINT ( 'NONE',  ( -57.48921356237308800, -27.52281430457095368, 5.000000000000000000 ) ) ;
#15355=CARTESIAN_POINT ( 'NONE',  ( -31.49999999999977973, -4.912538124160701791, 4.000000000000000000 ) ) ;
#15356=EDGE_CURVE ( 'NONE', #97811, #111424, #138095, .T. ) ;
#15357=DIRECTION ( 'NONE',  ( 0.6830127018922180770, -0.6830127018922204085, -0.2588190451025213501 ) ) ;
#15358=VERTEX_POINT ( 'NONE', #117042 ) ;
#15359=ORIENTED_EDGE ( 'NONE', *, *, #76985, .F. ) ;
#15360=DIRECTION ( 'NONE',  ( 0.6830127018922180770, -0.6830127018922204085, -0.2588190451025213501 ) ) ;
#15361=CARTESIAN_POINT ( 'NONE',  ( -14.51078643762690490, -27.52281430457045275, 5.000000000000000000 ) ) ;
#15362=CARTESIAN_POINT ( 'NONE',  ( -18.79289321881332242, 12.75929247661558819, 5.000000000000000000 ) ) ;
#15363=EDGE_CURVE ( 'NONE', #132813, #128314, #114872, .T. ) ;
#15365=VECTOR ( 'NONE', #30759, 1000.000000000000000 ) ;
#15366=AXIS2_PLACEMENT_3D ( 'NONE', #76202, #43565, #21815 ) ;
#15368=ORIENTED_EDGE ( 'NONE', *, *, #124552, .F. ) ;
#15369=DIRECTION ( 'NONE',  ( -0.7071067811865486830, -0.7071067811865464625, -0.000000000000000000 ) ) ;
#15371=PLANE ( 'NONE',  #98690 ) ;
#15373=ORIENTED_EDGE ( 'NONE', *, *, #97145, .T. ) ;
#15375=DIRECTION ( 'NONE',  ( -0.000000000000000000, -0.000000000000000000, 1.000000000000000000 ) ) ;
#15376=ORIENTED_EDGE ( 'NONE', *, *, #123795, .F. ) ;
#15378=EDGE_CURVE ( 'NONE', #110710, #5966, #126482, .T. ) ;
#15379=EDGE_LOOP ( 'NONE', ( #132397, #21798, #9511, #34737 ) ) ;
#15380=FACE_OUTER_BOUND ( 'NONE', #66183, .T. ) ;
#15382=EDGE_CURVE ( 'NONE', #87580, #102653, #106136, .T. ) ;
#15383=FACE_BOUND ( 'NONE', #86105, .T. ) ;
#15384=LINE ( 'NONE', #137218, #85004 ) ;
#15386=DIRECTION ( 'NONE',  ( 0.3543493200069163240, 0.000000000000000000, -0.9351131265310288487 ) ) ;
#15388=EDGE_CURVE ( 'NONE', #1058, #108205, #32188, .T. ) ;
#15389=CARTESIAN_POINT ( 'NONE',  ( 26.99999999999982236, -3.412538124160717778, 4.000000000000000000 ) ) ;
#15390=LINE ( 'NONE', #39346, #15848 ) ;
#15391=ORIENTED_EDGE ( 'NONE', *, *, #73426, .T. ) ;
#15392=CARTESIAN_POINT ( 'NONE',  ( 7.499999999999951150, 22.22500000000000142, 4.362957392718792349 ) ) ;
#15393=ORIENTED_EDGE ( 'NONE', *, *, #25342, .F. ) ;
#15394=ADVANCED_FACE ( 'NONE', ( #53967 ), #43779, .F. ) ;
#15395=ORIENTED_EDGE ( 'NONE', *, *, #122396, .F. ) ;
#15397=ORIENTED_EDGE ( 'NONE', *, *, #93138, .F. ) ;
#15398=CARTESIAN_POINT ( 'NONE',  ( 10.49999999999993605, 19.08746187583904330, 4.000000000000000000 ) ) ;
#15400=VERTEX_POINT ( 'NONE', #75701 ) ;
#15401=CARTESIAN_POINT ( 'NONE',  ( 24.20969143188526118, 6.176090689687629975, 5.000000000000000000 ) ) ;
#15402=AXIS2_PLACEMENT_3D ( 'NONE', #62467, #115361, #6591 ) ;
#15405=CARTESIAN_POINT ( 'NONE',  ( 25.49999999999982592, 9.431123077392085108, 4.000000000000000000 ) ) ;
#15406=PLANE ( 'NONE',  #71364 ) ;
#15407=DIRECTION ( 'NONE',  ( -0.7071067811865486830, -0.7071067811865464625, -0.000000000000000000 ) ) ;
#15408=DIRECTION ( 'NONE',  ( -0.7071067811865486830, -0.7071067811865464625, -0.000000000000000000 ) ) ;
#15409=CARTESIAN_POINT ( 'NONE',  ( -45.48921356237309510, -27.52281430457087197, 5.000000000000000000 ) ) ;
#15410=ORIENTED_EDGE ( 'NONE', *, *, #75777, .F. ) ;
#15411=ORIENTED_EDGE ( 'NONE', *, *, #69630, .F. ) ;
#15413=CARTESIAN_POINT ( 'NONE',  ( 18.04658813629533043, 14.25929247661557042, 18.84478104361323503 ) ) ;
#15414=ORIENTED_EDGE ( 'NONE', *, *, #24417, .T. ) ;
#15416=ORIENTED_EDGE ( 'NONE', *, *, #23546, .T. ) ;
#15417=CARTESIAN_POINT ( 'NONE',  ( -54.18398860626899705, 28.73617430169825226, 5.000000000000000000 ) ) ;
#15418=AXIS2_PLACEMENT_3D ( 'NONE', #10759, #20211, #32556 ) ;
#15419=EDGE_CURVE ( 'NONE', #57964, #86807, #85841, .T. ) ;
#15420=LINE ( 'NONE', #81466, #50769 ) ;
#15421=ORIENTED_EDGE ( 'NONE', *, *, #55307, .F. ) ;
#15422=DIRECTION ( 'NONE',  ( -0.3543493200069163240, 0.000000000000000000, -0.9351131265310288487 ) ) ;
#15425=LINE ( 'NONE', #93746, #102802 ) ;
#15426=ORIENTED_EDGE ( 'NONE', *, *, #31913, .T. ) ;
#15427=VECTOR ( 'NONE', #114871, 1000.000000000000000 ) ;
#15428=PLANE ( 'NONE',  #119808 ) ;
#15430=LINE ( 'NONE', #136522, #61406 ) ;
#15431=LINE ( 'NONE', #93035, #70387 ) ;
#15432=ORIENTED_EDGE ( 'NONE', *, *, #123711, .T. ) ;
#15433=PLANE ( 'NONE',  #35589 ) ;
#15434=ORIENTED_EDGE ( 'NONE', *, *, #84917, .F. ) ;
#15435=CARTESIAN_POINT ( 'NONE',  ( 0.000000000000000000, 0.000000000000000000, 5.000000000000000000 ) ) ;
#15436=CARTESIAN_POINT ( 'NONE',  ( -35.99451991528749772, 28.92564299267963079, 4.000000000000000000 ) ) ;
#15437=PLANE ( 'NONE',  #84137 ) ;
#15440=FACE_OUTER_BOUND ( 'NONE', #132918, .T. ) ;
#15441=FACE_OUTER_BOUND ( 'NONE', #116538, .T. ) ;
#15442=FACE_OUTER_BOUND ( 'NONE', #77158, .T. ) ;
#15443=ADVANCED_FACE ( 'NONE', ( #118467 ), #107593, .F. ) ;
#15444=EDGE_LOOP ( 'NONE', ( #62133, #61120, #142942, #109634 ) ) ;
#15445=LINE ( 'NONE', #59734, #55558 ) ;
#15446=DIRECTION ( 'NONE',  ( -0.7071067811865486830, -0.7071067811865464625, 0.000000000000000000 ) ) ;
#15448=DIRECTION ( 'NONE',  ( -0.6830127018922180770, -0.6830127018922204085, -0.2588190451025213501 ) ) ;
#15451=EDGE_LOOP ( 'NONE', ( #3645, #22840, #54968, #71558 ) ) ;
#15452=ORIENTED_EDGE ( 'NONE', *, *, #108130, .T. ) ;
#15453=DIRECTION ( 'NONE',  ( -0.7071067811865486830, 0.7071067811865464625, 0.000000000000000000 ) ) ;
#15454=CARTESIAN_POINT ( 'NONE',  ( 10.49999999999993250, -2.947814304570795851, 5.000000000000000000 ) ) ;
#15456=VECTOR ( 'NONE', #103640, 999.9999999999998863 ) ;
#15459=LINE ( 'NONE', #124262, #71414 ) ;
#15460=AXIS2_PLACEMENT_3D ( 'NONE', #548, #136074, #113599 ) ;
#15461=ADVANCED_FACE ( 'NONE', ( #40927 ), #86584, .F. ) ;
#15463=DIRECTION ( 'NONE',  ( -0.7071067811865486830, -0.7071067811865464625, 0.000000000000000000 ) ) ;
#15467=CARTESIAN_POINT ( 'NONE',  ( 34.92499999999998295, 6.856123077392344278, 4.000000000000000000 ) ) ;
#15468=VECTOR ( 'NONE', #499, 1000.000000000000227 ) ;
#15469=EDGE_CURVE ( 'NONE', #25609, #75083, #120589, .T. ) ;
#15470=DIRECTION ( 'NONE',  ( -0.7071067811865486830, 0.7071067811865464625, 0.000000000000000000 ) ) ;
#15471=VECTOR ( 'NONE', #126989, 999.9999999999998863 ) ;
#15472=PLANE ( 'NONE',  #8758 ) ;
#15473=EDGE_CURVE ( 'NONE', #77841, #44481, #134598, .T. ) ;
#15475=CARTESIAN_POINT ( 'NONE',  ( -26.00492477221178689, -5.240707523384232402, 12.38332538355501811 ) ) ;
#15478=VERTEX_POINT ( 'NONE', #7553 ) ;
#15479=EDGE_CURVE ( 'NONE', #122031, #20842, #98162, .T. ) ;
#15480=CARTESIAN_POINT ( 'NONE',  ( 24.18398860626899705, 28.73617430169804265, 5.000000000000000000 ) ) ;
#15482=PLANE ( 'NONE',  #63996 ) ;
#15483=CARTESIAN_POINT ( 'NONE',  ( 17.67183060077635304, -12.74070752338415247, 4.000000000000000000 ) ) ;
#15484=DIRECTION ( 'NONE',  ( -0.7071067811865487940, 0.7071067811865463515, 0.000000000000000000 ) ) ;
#15486=DIRECTION ( 'NONE',  ( -0.7071067811865486830, 0.7071067811865464625, 0.000000000000000000 ) ) ;
#15488=DIRECTION ( 'NONE',  ( 1.000000000000000000, 0.000000000000000000, 0.000000000000000000 ) ) ;
#15489=EDGE_LOOP ( 'NONE', ( #113541, #89443, #79077, #66892 ) ) ;
#15490=DIRECTION ( 'NONE',  ( 0.6830127018922181881, 0.6830127018922202975, -0.2588190451025214056 ) ) ;
#15492=VECTOR ( 'NONE', #54535, 1000.000000000000227 ) ;
#15493=DIRECTION ( 'NONE',  ( 0.7071067811865487940, -0.7071067811865463515, 0.000000000000000000 ) ) ;
#15494=EDGE_CURVE ( 'NONE', #88116, #90172, #11104, .T. ) ;
#15495=CARTESIAN_POINT ( 'NONE',  ( -34.45011844616455221, 12.00230414159383407, 5.000000000000000888 ) ) ;
#15497=VECTOR ( 'NONE', #117024, 1000.000000000000114 ) ;
#15498=LINE ( 'NONE', #138761, #87836 ) ;
#15499=VERTEX_POINT ( 'NONE', #80706 ) ;
#15500=ORIENTED_EDGE ( 'NONE', *, *, #8726, .T. ) ;
#15502=CARTESIAN_POINT ( 'NONE',  ( -0.5166543864104510275, 22.22500000000000142, 4.500000000000000888 ) ) ;
#15503=DIRECTION ( 'NONE',  ( 0.7071067811865487940, 0.7071067811865463515, 0.000000000000000000 ) ) ;
#15505=AXIS2_PLACEMENT_3D ( 'NONE', #94007, #59296, #15698 ) ;
#15507=CARTESIAN_POINT ( 'NONE',  ( 0.000000000000000000, 0.000000000000000000, 5.000000000000000000 ) ) ;
#15510=EDGE_CURVE ( 'NONE', #127280, #61991, #35791, .T. ) ;
#15512=DIRECTION ( 'NONE',  ( -0.7071067811865486830, 0.7071067811865464625, 0.000000000000000000 ) ) ;
#15513=VERTEX_POINT ( 'NONE', #66964 ) ;
#15514=ORIENTED_EDGE ( 'NONE', *, *, #89035, .T. ) ;
#15517=CARTESIAN_POINT ( 'NONE',  ( 4.499999999999962697, -4.912538124160703568, 4.000000000000000000 ) ) ;
#15518=AXIS2_PLACEMENT_3D ( 'NONE', #8432, #66453, #75198 ) ;
#15520=DIRECTION ( 'NONE',  ( -0.6830127018922180770, -0.6830127018922204085, -0.2588190451025213501 ) ) ;
#15521=CARTESIAN_POINT ( 'NONE',  ( -10.49999999999992895, 12.43112307739206024, 4.000000000000000000 ) ) ;
#15522=VERTEX_POINT ( 'NONE', #135784 ) ;
#15523=CARTESIAN_POINT ( 'NONE',  ( -24.18398860626899705, 28.73617430169804265, 5.000000000000000000 ) ) ;
#15525=CARTESIAN_POINT ( 'NONE',  ( 51.18398860626899705, 28.73617430169823095, 5.000000000000000000 ) ) ;
#15527=ORIENTED_EDGE ( 'NONE', *, *, #75952, .T. ) ;
#15528=ORIENTED_EDGE ( 'NONE', *, *, #113028, .F. ) ;
#15529=VECTOR ( 'NONE', #37175, 1000.000000000000000 ) ;
#15530=LINE ( 'NONE', #38758, #98473 ) ;
#15531=LINE ( 'NONE', #49669, #85828 ) ;
#15532=EDGE_CURVE ( 'NONE', #37315, #4279, #57531, .T. ) ;
#15534=CARTESIAN_POINT ( 'NONE',  ( -34.92500000000001137, 14.81665438641027777, 4.500000000000000888 ) ) ;
#15535=VERTEX_POINT ( 'NONE', #66255 ) ;
#15537=DIRECTION ( 'NONE',  ( 0.6830127018922180770, -0.6830127018922204085, -0.2588190451025213501 ) ) ;
#15538=LINE ( 'NONE', #81587, #72337 ) ;
#15540=EDGE_CURVE ( 'NONE', #68539, #59824, #80013, .T. ) ;
#15541=LINE ( 'NONE', #59823, #118455 ) ;
#15542=ORIENTED_EDGE ( 'NONE', *, *, #42849, .F. ) ;
#15544=DIRECTION ( 'NONE',  ( 0.6830127018922180770, -0.6830127018922204085, -0.2588190451025213501 ) ) ;
#15545=AXIS2_PLACEMENT_3D ( 'NONE', #56822, #100984, #79997 ) ;
#15546=EDGE_CURVE ( 'NONE', #6620, #86768, #67711, .T. ) ;
#15547=FACE_BOUND ( 'NONE', #84302, .T. ) ;
#15549=DIRECTION ( 'NONE',  ( 0.6830127018922181881, 0.6830127018922202975, -0.2588190451025214056 ) ) ;
#15550=LINE ( 'NONE', #29843, #22788 ) ;
#15551=FACE_OUTER_BOUND ( 'NONE', #131961, .T. ) ;
#15552=VECTOR ( 'NONE', #51810, 1000.000000000000114 ) ;
#15553=AXIS2_PLACEMENT_3D ( 'NONE', #13260, #22007, #35792 ) ;
#15554=PRODUCT_CONTEXT ( 'NONE', #45749, 'mechanical' ) ;
#15555=EDGE_LOOP ( 'NONE', ( #81322, #95138, #94211, #5333 ) ) ;
#15556=VECTOR ( 'NONE', #114509, 1000.000000000000000 ) ;
#15559=EDGE_LOOP ( 'NONE', ( #40652, #73120, #46849, #6586 ) ) ;
#15561=VECTOR ( 'NONE', #126631, 1000.000000000000227 ) ;
#15562=CARTESIAN_POINT ( 'NONE',  ( -1.499999999999990452, 21.05218569542895679, 5.000000000000000000 ) ) ;
#15563=LINE ( 'NONE', #106153, #124246 ) ;
#15564=DIRECTION ( 'NONE',  ( -0.7071067811865486830, -0.7071067811865464625, -0.000000000000000000 ) ) ;
#15566=LINE ( 'NONE', #50398, #22891 ) ;
#15567=ADVANCED_FACE ( 'NONE', ( #90872 ), #112603, .F. ) ;
#15568=CARTESIAN_POINT ( 'NONE',  ( 14.70025512860841133, -27.71228299555195917, 4.000000000000000000 ) ) ;
#15569=LINE ( 'NONE', #104017, #133762 ) ;
#15571=CARTESIAN_POINT ( 'NONE',  ( 26.99451991528749417, 28.92564299267956685, 4.000000000000000000 ) ) ;
#15572=CARTESIAN_POINT ( 'NONE',  ( 34.49999999999976552, 22.08746187583902554, 4.000000000000000000 ) ) ;
#15573=CARTESIAN_POINT ( 'NONE',  ( -10.49999999999992006, -10.91253812416064584, 4.000000000000000000 ) ) ;
#15574=EDGE_LOOP ( 'NONE', ( #124025, #15587, #4572, #25270 ) ) ;
#15575=FACE_OUTER_BOUND ( 'NONE', #15285, .T. ) ;
#15576=LINE ( 'NONE', #38112, #69728 ) ;
#15577=ORIENTED_EDGE ( 'NONE', *, *, #86580, .F. ) ;
#15578=ADVANCED_FACE ( 'NONE', ( #11834 ), #56839, .T. ) ;
#15580=ADVANCED_FACE ( 'NONE', ( #77837 ), #111897, .F. ) ;
#15581=VERTEX_POINT ( 'NONE', #45240 ) ;
#15583=EDGE_LOOP ( 'NONE', ( #46035, #47606, #61467, #25881, #101766 ) ) ;
#15584=VECTOR ( 'NONE', #35509, 1000.000000000000000 ) ;
#15587=ORIENTED_EDGE ( 'NONE', *, *, #44846, .T. ) ;
#15588=DIRECTION ( 'NONE',  ( -0.6830127018922180770, -0.6830127018922204085, -0.2588190451025213501 ) ) ;
#15591=AXIS2_PLACEMENT_3D ( 'NONE', #22847, #67114, #36605 ) ;
#15592=LINE ( 'NONE', #37400, #26682 ) ;
#15593=DIRECTION ( 'NONE',  ( 0.7071067811865487940, 0.7071067811865463515, 0.000000000000000000 ) ) ;
#15594=VERTEX_POINT ( 'NONE', #958 ) ;
#15595=EDGE_LOOP ( 'NONE', ( #62373, #114538, #108145, #87338 ) ) ;
#15597=CARTESIAN_POINT ( 'NONE',  ( -51.18398860626899705, 28.73617430169823095, 5.000000000000000000 ) ) ;
#15598=DIRECTION ( 'NONE',  ( -0.7071067811865487940, 0.7071067811865463515, -0.000000000000000000 ) ) ;
#15599=ORIENTED_EDGE ( 'NONE', *, *, #16096, .T. ) ;
#15601=ORIENTED_EDGE ( 'NONE', *, *, #43557, .T. ) ;
#15604=ORIENTED_EDGE ( 'NONE', *, *, #128014, .F. ) ;
#15605=VERTEX_POINT ( 'NONE', #99556 ) ;
#15607=CARTESIAN_POINT ( 'NONE',  ( 20.70025512860841133, -27.71228299555191654, 4.000000000000000000 ) ) ;
#15608=LINE ( 'NONE', #78789, #56435 ) ;
#15609=CARTESIAN_POINT ( 'NONE',  ( -14.70822291016943240, -15.74070752338411694, 19.73771281079093853 ) ) ;
#15610=LINE ( 'NONE', #58514, #55823 ) ;
#15611=ORIENTED_EDGE ( 'NONE', *, *, #110546, .T. ) ;
#15612=PLANE ( 'NONE',  #77228 ) ;
#15614=CARTESIAN_POINT ( 'NONE',  ( 34.82816939922329169, 18.75929247661552424, 4.000000000000000000 ) ) ;
#15615=ADVANCED_FACE ( 'NONE', ( #111141 ), #55381, .F. ) ;
#15616=DIRECTION ( 'NONE',  ( -0.000000000000000000, 0.3543493200069153248, 0.9351131265310292928 ) ) ;
#15617=VECTOR ( 'NONE', #18804, 999.9999999999998863 ) ;
#15619=ORIENTED_EDGE ( 'NONE', *, *, #58860, .F. ) ;
#15621=EDGE_LOOP ( 'NONE', ( #24071, #124112, #130015, #100593 ) ) ;
#15622=ORIENTED_EDGE ( 'NONE', *, *, #21670, .T. ) ;
#15623=FACE_OUTER_BOUND ( 'NONE', #49963, .T. ) ;
#15624=FACE_OUTER_BOUND ( 'NONE', #1502, .T. ) ;
#15626=CARTESIAN_POINT ( 'NONE',  ( 18.48921356237309510, -27.52281430457068367, 5.000000000000000000 ) ) ;
#15627=LINE ( 'NONE', #49042, #28846 ) ;
#15629=EDGE_CURVE ( 'NONE', #28732, #18685, #123512, .T. ) ;
#15631=ADVANCED_FACE ( 'NONE', ( #3111 ), #134369, .F. ) ;
#15634=VECTOR ( 'NONE', #133068, 999.9999999999998863 ) ;
#15635=DIRECTION ( 'NONE',  ( -0.6830127018922180770, -0.6830127018922204085, -0.2588190451025213501 ) ) ;
#15636=CARTESIAN_POINT ( 'NONE',  ( -2.999999999999969802, -1.447814304570815169, 5.000000000000000000 ) ) ;
#15637=DIRECTION ( 'NONE',  ( -0.7071067811865487940, 0.7071067811865463515, -0.000000000000000000 ) ) ;
#15638=EDGE_LOOP ( 'NONE', ( #51746, #58305, #47434, #67401 ) ) ;
#15640=ORIENTED_EDGE ( 'NONE', *, *, #130594, .T. ) ;
#15641=AXIS2_PLACEMENT_3D ( 'NONE', #70084, #114248, #60628 ) ;
#15642=CARTESIAN_POINT ( 'NONE',  ( 11.99999999999992362, 4.552185695429119328, 5.000000000000000000 ) ) ;
#15643=FACE_OUTER_BOUND ( 'NONE', #65132, .T. ) ;
#15644=ORIENTED_EDGE ( 'NONE', *, *, #55401, .F. ) ;
#15647=PLANE ( 'NONE',  #104206 ) ;
#15648=DIRECTION ( 'NONE',  ( -0.3543493200069162685, -0.000000000000000000, -0.9351131265310288487 ) ) ;
#15649=EDGE_LOOP ( 'NONE', ( #50438, #43600, #87061, #78003 ) ) ;
#15650=PLANE ( 'NONE',  #110983 ) ;
#15651=EDGE_LOOP ( 'NONE', ( #143069, #49667, #33818, #96759 ) ) ;
#15653=EDGE_LOOP ( 'NONE', ( #105804, #45277, #59698, #88455 ) ) ;
#15654=VECTOR ( 'NONE', #5773, 1000.000000000000000 ) ;
#15655=VECTOR ( 'NONE', #45779, 1000.000000000000000 ) ;
#15656=CARTESIAN_POINT ( 'NONE',  ( 18.48921356237309510, -27.52281430457068367, 5.000000000000000000 ) ) ;
#15659=PLANE ( 'NONE',  #13910 ) ;
#15661=ORIENTED_EDGE ( 'NONE', *, *, #119085, .T. ) ;
#15662=CARTESIAN_POINT ( 'NONE',  ( 39.18398860626899705, 28.73617430169814568, 5.000000000000000000 ) ) ;
#15663=DIRECTION ( 'NONE',  ( -0.7071067811865486830, 0.7071067811865464625, 0.000000000000000000 ) ) ;
#15664=LINE ( 'NONE', #59953, #6677 ) ;
#15666=CARTESIAN_POINT ( 'NONE',  ( -15.44591897758377108, -1.592173378680612927, 4.204195949441833946 ) ) ;
#15667=ADVANCED_FACE ( 'NONE', ( #4477 ), #40071, .F. ) ;
#15668=CARTESIAN_POINT ( 'NONE',  ( -39.48921356237310221, -27.52281430457082934, 5.000000000000000000 ) ) ;
#15671=ORIENTED_EDGE ( 'NONE', *, *, #123003, .F. ) ;
#15673=FACE_OUTER_BOUND ( 'NONE', #67810, .T. ) ;
#15674=ADVANCED_FACE ( 'NONE', ( #27009 ), #25574, .F. ) ;
#15675=DIRECTION ( 'NONE',  ( -0.3543493200069162685, -0.000000000000000000, -0.9351131265310288487 ) ) ;
#15676=LINE ( 'NONE', #104126, #66435 ) ;
#15677=ORIENTED_EDGE ( 'NONE', *, *, #124962, .F. ) ;
#15678=CARTESIAN_POINT ( 'NONE',  ( -2.994519915287485734, 28.92564299267940342, 4.000000000000000000 ) ) ;
#15680=DIRECTION ( 'NONE',  ( -0.6830127018922180770, -0.6830127018922204085, -0.2588190451025213501 ) ) ;
#15681=CARTESIAN_POINT ( 'NONE',  ( 25.49999999999982236, 13.08746187583911436, 4.000000000000000000 ) ) ;
#15682=CARTESIAN_POINT ( 'NONE',  ( -14.67183060077636370, -21.74070752338405299, 4.000000000000000000 ) ) ;
#15683=CARTESIAN_POINT ( 'NONE',  ( 5.292986735706907808, -21.74070752338406365, 4.999753212805221558 ) ) ;
#15684=ORIENTED_EDGE ( 'NONE', *, *, #25938, .T. ) ;
#15685=EDGE_CURVE ( 'NONE', #12429, #39954, #37176, .T. ) ;
#15686=CARTESIAN_POINT ( 'NONE',  ( -29.27718569542920335, -21.72500000000000142, 5.000000000000000000 ) ) ;
#15688=FACE_OUTER_BOUND ( 'NONE', #44218, .T. ) ;
#15689=CARTESIAN_POINT ( 'NONE',  ( 9.183988606268997046, 28.73617430169793607, 5.000000000000000000 ) ) ;
#15691=VERTEX_POINT ( 'NONE', #70569 ) ;
#15693=ORIENTED_EDGE ( 'NONE', *, *, #1862, .F. ) ;
#15694=ORIENTED_EDGE ( 'NONE', *, *, #5491, .T. ) ;
#15696=VERTEX_POINT ( 'NONE', #26311 ) ;
#15697=DIRECTION ( 'NONE',  ( -0.6830127018922181881, 0.6830127018922202975, -0.2588190451025214056 ) ) ;
#15698=DIRECTION ( 'NONE',  ( 0.7071067811865487940, 0.7071067811865463515, 0.000000000000000000 ) ) ;
#15700=DIRECTION ( 'NONE',  ( -0.7071067811865486830, 0.7071067811865464625, 0.000000000000000000 ) ) ;
#15701=ORIENTED_EDGE ( 'NONE', *, *, #65583, .F. ) ;
#15702=CARTESIAN_POINT ( 'NONE',  ( 34.92499999999998295, 10.33457404400606450, 0.4942731178106110068 ) ) ;
#15703=CARTESIAN_POINT ( 'NONE',  ( -33.79289321881321939, 15.75929247661555976, 5.000000000000000000 ) ) ;
#15705=VERTEX_POINT ( 'NONE', #6637 ) ;
#15706=DIRECTION ( 'NONE',  ( 0.7071067811865486830, -0.7071067811865464625, -0.000000000000000000 ) ) ;
#15707=DIRECTION ( 'NONE',  ( 0.7071067811865487940, 0.7071067811865463515, 0.000000000000000000 ) ) ;
#15708=LINE ( 'NONE', #123835, #93249 ) ;
#15709=EDGE_LOOP ( 'NONE', ( #41225, #73345, #24701, #63052 ) ) ;
#15710=ORIENTED_EDGE ( 'NONE', *, *, #128128, .T. ) ;
#15712=CARTESIAN_POINT ( 'NONE',  ( -34.92500000000001137, 22.22500000000000142, 4.000000000000000000 ) ) ;
#15713=PLANE ( 'NONE',  #122559 ) ;
#15714=LINE ( 'NONE', #50540, #41973 ) ;
#15715=DIRECTION ( 'NONE',  ( -0.6830127018922181881, 0.6830127018922202975, -0.2588190451025214056 ) ) ;
#15716=DIRECTION ( 'NONE',  ( 0.7071067811865487940, 0.7071067811865463515, 0.000000000000000000 ) ) ;
#15717=DIRECTION ( 'NONE',  ( -0.7071067811865486830, -0.7071067811865464625, -0.000000000000000000 ) ) ;
#15719=ORIENTED_EDGE ( 'NONE', *, *, #131425, .F. ) ;
#15720=VECTOR ( 'NONE', #13109, 1000.000000000000000 ) ;
#15721=ORIENTED_EDGE ( 'NONE', *, *, #24865, .T. ) ;
#15722=VERTEX_POINT ( 'NONE', #71255 ) ;
#15723=EDGE_CURVE ( 'NONE', #111351, #19902, #138647, .T. ) ;
#15724=CARTESIAN_POINT ( 'NONE',  ( 11.99999999999991829, -18.41253812416056945, 4.000000000000000000 ) ) ;
#15728=CARTESIAN_POINT ( 'NONE',  ( -8.700255128608413102, -27.71228299555199825, 4.000000000000000000 ) ) ;
#15729=DIRECTION ( 'NONE',  ( -0.3543493200069162685, -0.000000000000000000, -0.9351131265310288487 ) ) ;
#15731=DIRECTION ( 'NONE',  ( 0.7071067811865487940, 0.7071067811865463515, 0.000000000000000000 ) ) ;
#15732=ORIENTED_EDGE ( 'NONE', *, *, #78242, .T. ) ;
#15733=CARTESIAN_POINT ( 'NONE',  ( 34.92499999999998295, 22.22500000000000142, 4.000000000000000000 ) ) ;
#15734=VECTOR ( 'NONE', #48073, 1000.000000000000000 ) ;
#15735=ORIENTED_EDGE ( 'NONE', *, *, #1926, .T. ) ;
#15736=EDGE_CURVE ( 'NONE', #40291, #123040, #50210, .T. ) ;
#15737=DIRECTION ( 'NONE',  ( -0.000000000000000000, 0.3543493200069153248, 0.9351131265310292928 ) ) ;
#15738=EDGE_LOOP ( 'NONE', ( #81946, #120299, #87573, #60609 ) ) ;
#15739=ORIENTED_EDGE ( 'NONE', *, *, #64994, .F. ) ;
#15740=CARTESIAN_POINT ( 'NONE',  ( -48.29974487139158867, -27.71228299555239971, 4.000000000000000000 ) ) ;
#15741=EDGE_CURVE ( 'NONE', #3283, #126278, #93706, .T. ) ;
#15742=ORIENTED_EDGE ( 'NONE', *, *, #74351, .T. ) ;
#15745=VECTOR ( 'NONE', #69136, 1000.000000000000000 ) ;
#15746=ORIENTED_EDGE ( 'NONE', *, *, #125818, .F. ) ;
#15747=VECTOR ( 'NONE', #17390, 1000.000000000000000 ) ;
#15752=EDGE_CURVE ( 'NONE', #12370, #141174, #59671, .T. ) ;
#15753=CARTESIAN_POINT ( 'NONE',  ( 19.49999999999987210, -12.08601207473287253, -10.46905243149098474 ) ) ;
#15755=DIRECTION ( 'NONE',  ( -0.7071067811865486830, -0.7071067811865464625, -0.000000000000000000 ) ) ;
#15756=DIRECTION ( 'NONE',  ( 0.3543493200069162685, -0.000000000000000000, -0.9351131265310288487 ) ) ;
#15758=DIRECTION ( 'NONE',  ( 1.000000000000000000, 0.000000000000000000, 0.000000000000000000 ) ) ;
#15759=EDGE_CURVE ( 'NONE', #38066, #132490, #82146, .T. ) ;
#15761=CARTESIAN_POINT ( 'NONE',  ( 24.66594027184343219, -22.22500000000000142, -17.58123489532666639 ) ) ;
#15762=VERTEX_POINT ( 'NONE', #39342 ) ;
#15763=CARTESIAN_POINT ( 'NONE',  ( 0.000000000000000000, 0.000000000000000000, 5.000000000000000000 ) ) ;
#15764=LINE ( 'NONE', #104225, #86925 ) ;
#15765=ORIENTED_EDGE ( 'NONE', *, *, #81814, .T. ) ;
#15766=ORIENTED_EDGE ( 'NONE', *, *, #97030, .T. ) ;
#15767=AXIS2_PLACEMENT_3D ( 'NONE', #58739, #15830, #115156 ) ;
#15768=CARTESIAN_POINT ( 'NONE',  ( -28.49999999999980815, 14.14708470758588632, -0.5283514160165899698 ) ) ;
#15769=ADVANCED_FACE ( 'NONE', ( #83561 ), #127774, .T. ) ;
#15770=VERTEX_POINT ( 'NONE', #18238 ) ;
#15771=VECTOR ( 'NONE', #60468, 1000.000000000000000 ) ;
#15773=CARTESIAN_POINT ( 'NONE',  ( -11.48334561358947070, 22.22500000000000142, 4.500000000000000888 ) ) ;
#15774=AXIS2_PLACEMENT_3D ( 'NONE', #55776, #77536, #110811 ) ;
#15775=FACE_OUTER_BOUND ( 'NONE', #32601, .T. ) ;
#15776=CARTESIAN_POINT ( 'NONE',  ( -14.99999999999990230, 7.559798855135676732, 4.979909187984716823 ) ) ;
#15777=ORIENTED_EDGE ( 'NONE', *, *, #70554, .T. ) ;
#15778=ORIENTED_EDGE ( 'NONE', *, *, #38962, .F. ) ;
#15781=DIRECTION ( 'NONE',  ( -0.6830127018922181881, 0.6830127018922202975, -0.2588190451025214056 ) ) ;
#15782=DIRECTION ( 'NONE',  ( 0.000000000000000000, 0.000000000000000000, -1.000000000000000000 ) ) ;
#15784=VERTEX_POINT ( 'NONE', #29853 ) ;
#15789=LINE ( 'NONE', #37614, #46470 ) ;
#15790=PLANE ( 'NONE',  #105237 ) ;
#15791=VECTOR ( 'NONE', #23840, 1000.000000000000000 ) ;
#15792=FACE_OUTER_BOUND ( 'NONE', #109042, .T. ) ;
#15793=CARTESIAN_POINT ( 'NONE',  ( -34.92500000000001137, 21.00612307739172024, 4.000000000000000000 ) ) ;
#15794=VECTOR ( 'NONE', #321, 1000.000000000000000 ) ;
#15796=EDGE_CURVE ( 'NONE', #103206, #54270, #63937, .T. ) ;
#15797=DIRECTION ( 'NONE',  ( -0.7071067811865487940, 0.7071067811865463515, -0.000000000000000000 ) ) ;
#15798=DIRECTION ( 'NONE',  ( 0.3543493200069162685, -0.000000000000000000, -0.9351131265310288487 ) ) ;
#15799=DIRECTION ( 'NONE',  ( 0.6830127018922180770, -0.6830127018922204085, -0.2588190451025213501 ) ) ;
#15800=CARTESIAN_POINT ( 'NONE',  ( -7.499999999999951150, 6.277155672890267546, -3.510561720658922802 ) ) ;
#15801=ORIENTED_EDGE ( 'NONE', *, *, #27864, .T. ) ;
#15802=CARTESIAN_POINT ( 'NONE',  ( -8.510786437626906675, -27.52281430457049183, 5.000000000000000000 ) ) ;
#15803=DIRECTION ( 'NONE',  ( 0.3543493200069163240, -0.000000000000000000, 0.9351131265310288487 ) ) ;
#15804=ADVANCED_FACE ( 'NONE', ( #142226 ), #54502, .F. ) ;
#15805=ORIENTED_EDGE ( 'NONE', *, *, #1110, .T. ) ;
#15806=FACE_OUTER_BOUND ( 'NONE', #127568, .T. ) ;
#15807=DIRECTION ( 'NONE',  ( -1.000000000000000000, 0.000000000000000000, 0.000000000000000000 ) ) ;
#15809=ADVANCED_FACE ( 'NONE', ( #108107 ), #8771, .F. ) ;
#15810=ORIENTED_EDGE ( 'NONE', *, *, #9440, .T. ) ;
#15811=ADVANCED_FACE ( 'NONE', ( #98681 ), #53029, .F. ) ;
#15812=LINE ( 'NONE', #49240, #125591 ) ;
#15814=CARTESIAN_POINT ( 'NONE',  ( 17.67183060077634593, -18.74070752338409918, 4.000000000000000000 ) ) ;
#15815=VERTEX_POINT ( 'NONE', #119013 ) ;
#15816=DIRECTION ( 'NONE',  ( -0.000000000000000000, 0.3543493200069153248, 0.9351131265310292928 ) ) ;
#15818=DIRECTION ( 'NONE',  ( 0.7071067811865487940, 0.7071067811865463515, 0.000000000000000000 ) ) ;
#15822=CARTESIAN_POINT ( 'NONE',  ( -23.70025512860841133, -27.71228299555189523, 4.000000000000000000 ) ) ;
#15823=EDGE_CURVE ( 'NONE', #32577, #77379, #18993, .T. ) ;
#15824=LINE ( 'NONE', #6370, #113391 ) ;
#15825=DIRECTION ( 'NONE',  ( 0.7071067811865487940, 0.7071067811865463515, 0.000000000000000000 ) ) ;
#15826=PLANE ( 'NONE',  #51822 ) ;
#15827=CARTESIAN_POINT ( 'NONE',  ( -4.499999999999970690, 18.05218569542898521, 5.000000000000000000 ) ) ;
#15830=DIRECTION ( 'NONE',  ( -0.6830127018922181881, 0.6830127018922202975, -0.2588190451025214056 ) ) ;
#15832=DIRECTION ( 'NONE',  ( 0.6830127018922180770, -0.6830127018922204085, -0.2588190451025213501 ) ) ;
#15833=CARTESIAN_POINT ( 'NONE',  ( -31.49999999999977973, 22.01701374228153085, 2.453858888625704004 ) ) ;
#15834=ORIENTED_EDGE ( 'NONE', *, *, #123252, .F. ) ;
#15835=ORIENTED_EDGE ( 'NONE', *, *, #44736, .F. ) ;
#15837=ORIENTED_EDGE ( 'NONE', *, *, #131598, .T. ) ;
#15838=VERTEX_POINT ( 'NONE', #40760 ) ;
#15840=DIRECTION ( 'NONE',  ( 0.7071067811865486830, -0.7071067811865464625, -0.000000000000000000 ) ) ;
#15841=FACE_OUTER_BOUND ( 'NONE', #102912, .T. ) ;
#15843=VECTOR ( 'NONE', #13620, 1000.000000000000000 ) ;
#15845=VECTOR ( 'NONE', #115396, 1000.000000000000000 ) ;
#15846=LINE ( 'NONE', #6391, #34775 ) ;
#15848=VECTOR ( 'NONE', #94404, 1000.000000000000000 ) ;
#15849=DIRECTION ( 'NONE',  ( -0.7071067811865486830, -0.7071067811865464625, 0.000000000000000000 ) ) ;
#15852=FACE_OUTER_BOUND ( 'NONE', #36394, .T. ) ;
#15853=CARTESIAN_POINT ( 'NONE',  ( 1.499999999999994449, -13.53360074219760456, 5.000000000000000000 ) ) ;
#15854=PLANE ( 'NONE',  #114232 ) ;
#15855=EDGE_CURVE ( 'NONE', #138242, #128760, #129895, .T. ) ;
#15856=DIRECTION ( 'NONE',  ( -0.6830127018922180770, -0.6830127018922204085, -0.2588190451025213501 ) ) ;
#15858=DIRECTION ( 'NONE',  ( 0.6830127018922181881, 0.6830127018922202975, -0.2588190451025214056 ) ) ;
#15859=VECTOR ( 'NONE', #93120, 1000.000000000000227 ) ;
#15860=CARTESIAN_POINT ( 'NONE',  ( 14.99999999999989519, 10.21212019023810491, -2.019456568337833602 ) ) ;
#15863=EDGE_CURVE ( 'NONE', #116077, #140375, #118286, .T. ) ;
#15864=VERTEX_POINT ( 'NONE', #96515 ) ;
#15867=VERTEX_POINT ( 'NONE', #140753 ) ;
#15869=AXIS2_PLACEMENT_3D ( 'NONE', #140189, #128595, #83692 ) ;
#15871=VERTEX_POINT ( 'NONE', #85660 ) ;
#15872=EDGE_CURVE ( 'NONE', #91794, #25131, #19697, .T. ) ;
#15873=LINE ( 'NONE', #103621, #39766 ) ;
#15874=DIRECTION ( 'NONE',  ( -0.000000000000000000, 0.3543493200069153248, 0.9351131265310292928 ) ) ;
#15875=VECTOR ( 'NONE', #68526, 1000.000000000000000 ) ;
#15877=ORIENTED_EDGE ( 'NONE', *, *, #73001, .T. ) ;
#15878=CARTESIAN_POINT ( 'NONE',  ( -12.29974487139158512, -27.71228299555214747, 4.000000000000000000 ) ) ;
#15879=ORIENTED_EDGE ( 'NONE', *, *, #33602, .F. ) ;
#15880=CARTESIAN_POINT ( 'NONE',  ( 3.489213562373097322, -27.52281430457057709, 5.000000000000000000 ) ) ;
#15881=VECTOR ( 'NONE', #21769, 1000.000000000000227 ) ;
#15882=PLANE ( 'NONE',  #17098 ) ;
#15883=CARTESIAN_POINT ( 'NONE',  ( -24.62910658713767731, 1.050808743928695277, 4.662926800793053772 ) ) ;
#15884=AXIS2_PLACEMENT_3D ( 'NONE', #117517, #107377, #51593 ) ;
#15885=VECTOR ( 'NONE', #38335, 999.9999999999998863 ) ;
#15886=VECTOR ( 'NONE', #110673, 1000.000000000000000 ) ;
#15889=EDGE_LOOP ( 'NONE', ( #31574, #67961, #122767, #89448 ) ) ;
#15890=DIRECTION ( 'NONE',  ( 0.7071067811865487940, 0.7071067811865463515, -0.000000000000000000 ) ) ;
#15893=VECTOR ( 'NONE', #139925, 1000.000000000000000 ) ;
#15894=DIRECTION ( 'NONE',  ( -0.7071067811865487940, 0.7071067811865463515, -0.000000000000000000 ) ) ;
#15896=ORIENTED_EDGE ( 'NONE', *, *, #43829, .F. ) ;
#15899=ORIENTED_EDGE ( 'NONE', *, *, #122102, .F. ) ;
#15900=EDGE_CURVE ( 'NONE', #4623, #101006, #20394, .T. ) ;
#15901=EDGE_CURVE ( 'NONE', #71584, #76991, #99375, .T. ) ;
#15902=ORIENTED_EDGE ( 'NONE', *, *, #135201, .F. ) ;
#15904=DIRECTION ( 'NONE',  ( 0.7071067811865487940, 0.7071067811865463515, 0.000000000000000000 ) ) ;
#15905=CARTESIAN_POINT ( 'NONE',  ( 0.000000000000000000, 0.000000000000000000, 5.000000000000000000 ) ) ;
#15906=ORIENTED_EDGE ( 'NONE', *, *, #103119, .T. ) ;
#15908=CARTESIAN_POINT ( 'NONE',  ( 12.29974487139158512, -27.71228299555214747, 4.000000000000000000 ) ) ;
#15909=CARTESIAN_POINT ( 'NONE',  ( -14.14994871458967474, -8.240707523384186217, 17.25253755692235558 ) ) ;
#15910=EDGE_CURVE ( 'NONE', #108316, #48577, #66087, .T. ) ;
#15911=LINE ( 'NONE', #6458, #46460 ) ;
#15912=FACE_BOUND ( 'NONE', #4223, .T. ) ;
#15913=ORIENTED_EDGE ( 'NONE', *, *, #84694, .T. ) ;
#15914=DIRECTION ( 'NONE',  ( 0.3543493200069162685, -0.000000000000000000, -0.9351131265310288487 ) ) ;
#15915=ADVANCED_FACE ( 'NONE', ( #13086 ), #77674, .F. ) ;
#15916=PLANE ( 'NONE',  #85134 ) ;
#15918=VERTEX_POINT ( 'NONE', #112431 ) ;
#15919=DIRECTION ( 'NONE',  ( 0.7071067811865487940, 0.7071067811865463515, 0.000000000000000000 ) ) ;
#15920=ORIENTED_EDGE ( 'NONE', *, *, #126161, .T. ) ;
#15921=EDGE_LOOP ( 'NONE', ( #58284, #68166, #136066, #54622 ) ) ;
#15922=ORIENTED_EDGE ( 'NONE', *, *, #124910, .F. ) ;
#15923=EDGE_CURVE ( 'NONE', #4732, #53545, #123331, .T. ) ;
#15924=ADVANCED_FACE ( 'NONE', ( #13793 ), #78381, .F. ) ;
#15927=LINE ( 'NONE', #4308, #6679 ) ;
#15928=CARTESIAN_POINT ( 'NONE',  ( -28.49999999999979039, -14.94781430457067906, 5.000000000000000000 ) ) ;
#15930=EDGE_CURVE ( 'NONE', #27998, #68281, #79125, .T. ) ;
#15932=PLANE ( 'NONE',  #69068 ) ;
#15933=DIRECTION ( 'NONE',  ( -0.6830127018922181881, 0.6830127018922202975, -0.2588190451025214056 ) ) ;
#15935=CARTESIAN_POINT ( 'NONE',  ( -34.49999999999975131, 19.46425560840030400, 4.994342998332171213 ) ) ;
#15936=CARTESIAN_POINT ( 'NONE',  ( 63.18398860626900415, 28.73617430169831621, 5.000000000000000000 ) ) ;
#15937=CARTESIAN_POINT ( 'NONE',  ( -24.18398860626899705, 28.73617430169804265, 5.000000000000000000 ) ) ;
#15938=CARTESIAN_POINT ( 'NONE',  ( 0.1839886062690032631, 28.73617430169787568, 5.000000000000000000 ) ) ;
#15939=VERTEX_POINT ( 'NONE', #76979 ) ;
#15940=ORIENTED_EDGE ( 'NONE', *, *, #68289, .T. ) ;
#15941=AXIS2_PLACEMENT_3D ( 'NONE', #133454, #110938, #108082 ) ;
#15942=ORIENTED_EDGE ( 'NONE', *, *, #7701, .T. ) ;
#15945=VECTOR ( 'NONE', #127972, 1000.000000000000000 ) ;
#15946=EDGE_CURVE ( 'NONE', #12209, #59656, #110256, .T. ) ;
#15947=AXIS2_PLACEMENT_3D ( 'NONE', #111982, #101074, #1725 ) ;
#15949=VECTOR ( 'NONE', #128618, 1000.000000000000000 ) ;
#15950=AXIS2_PLACEMENT_3D ( 'NONE', #611, #77510, #22348 ) ;
#15951=VERTEX_POINT ( 'NONE', #11648 ) ;
#15952=LINE ( 'NONE', #137071, #106969 ) ;
#15954=DIRECTION ( 'NONE',  ( -0.000000000000000000, 0.3543493200069153248, 0.9351131265310292928 ) ) ;
#15955=ORIENTED_EDGE ( 'NONE', *, *, #126042, .T. ) ;
#15956=CARTESIAN_POINT ( 'NONE',  ( -45.18398860626900415, 28.73617430169818832, 5.000000000000000000 ) ) ;
#15959=ORIENTED_EDGE ( 'NONE', *, *, #54328, .F. ) ;
#15961=FACE_OUTER_BOUND ( 'NONE', #3058, .T. ) ;
#15963=EDGE_LOOP ( 'NONE', ( #10213, #111816, #125433 ) ) ;
#15965=LINE ( 'NONE', #60257, #100876 ) ;
#15966=DIRECTION ( 'NONE',  ( -0.7071067811865486830, -0.7071067811865464625, 0.000000000000000000 ) ) ;
#15967=LINE ( 'NONE', #118148, #92857 ) ;
#15968=ORIENTED_EDGE ( 'NONE', *, *, #21836, .F. ) ;
#15969=ADVANCED_FACE ( 'NONE', ( #113124 ), #111720, .F. ) ;
#15970=ORIENTED_EDGE ( 'NONE', *, *, #97633, .F. ) ;
#15971=CARTESIAN_POINT ( 'NONE',  ( -39.48921356237310221, -27.52281430457082934, 5.000000000000000000 ) ) ;
#15972=EDGE_LOOP ( 'NONE', ( #678, #93222, #86308, #127397 ) ) ;
#15973=AXIS2_PLACEMENT_3D ( 'NONE', #118174, #64540, #97124 ) ;
#15974=LINE ( 'NONE', #82716, #62577 ) ;
#15975=VECTOR ( 'NONE', #88677, 999.9999999999998863 ) ;
#15976=PLANE ( 'NONE',  #6922 ) ;
#15977=CARTESIAN_POINT ( 'NONE',  ( -6.299744871391586898, -27.71228299555210484, 4.000000000000000000 ) ) ;
#15979=LINE ( 'NONE', #138524, #7810 ) ;
#15981=EDGE_CURVE ( 'NONE', #23291, #113319, #22526, .T. ) ;
#15982=LINE ( 'NONE', #104448, #127012 ) ;
#15983=VECTOR ( 'NONE', #59091, 1000.000000000000000 ) ;
#15984=EDGE_CURVE ( 'NONE', #113440, #71320, #783, .T. ) ;
#15985=DIRECTION ( 'NONE',  ( -0.7071067811865487940, 0.7071067811865463515, -0.000000000000000000 ) ) ;
#15986=DIRECTION ( 'NONE',  ( 0.000000000000000000, -1.000000000000000000, 0.000000000000000000 ) ) ;
#15988=CARTESIAN_POINT ( 'NONE',  ( -23.99999999999982592, 11.96639925780213964, 5.000000000000000000 ) ) ;
#15990=CARTESIAN_POINT ( 'NONE',  ( 14.99451991528749595, 28.92564299267948513, 4.000000000000000000 ) ) ;
#15991=VECTOR ( 'NONE', #102556, 1000.000000000000000 ) ;
#15993=ORIENTED_EDGE ( 'NONE', *, *, #77275, .F. ) ;
#15994=VECTOR ( 'NONE', #45687, 999.9999999999998863 ) ;
#15995=DIRECTION ( 'NONE',  ( -0.3543493200069162685, -0.000000000000000000, -0.9351131265310288487 ) ) ;
#15996=ORIENTED_EDGE ( 'NONE', *, *, #52146, .T. ) ;
#15997=VERTEX_POINT ( 'NONE', #12386 ) ;
#15998=FACE_OUTER_BOUND ( 'NONE', #29789, .T. ) ;
#15999=AXIS2_PLACEMENT_3D ( 'NONE', #67246, #47674, #133926 ) ;
#16001=EDGE_LOOP ( 'NONE', ( #131871, #119552, #61149, #29924 ) ) ;
#16002=CARTESIAN_POINT ( 'NONE',  ( 36.29974487139159578, -27.71228299555231445, 4.000000000000000000 ) ) ;
#16003=VECTOR ( 'NONE', #55244, 1000.000000000000000 ) ;
#16004=DIRECTION ( 'NONE',  ( -0.7071067811865487940, 0.7071067811865463515, -0.000000000000000000 ) ) ;
#16006=VERTEX_POINT ( 'NONE', #79850 ) ;
#16009=DIRECTION ( 'NONE',  ( 0.3543493200069162685, -0.000000000000000000, -0.9351131265310288487 ) ) ;
#16011=CARTESIAN_POINT ( 'NONE',  ( 26.29289321881327623, 14.25929247661557753, 5.000000000000000000 ) ) ;
#16014=DIRECTION ( 'NONE',  ( 0.3543493200069162685, -0.000000000000000000, -0.9351131265310288487 ) ) ;
#16015=ADVANCED_FACE ( 'NONE', ( #100833 ), #134930, .T. ) ;
#16016=LINE ( 'NONE', #5140, #132274 ) ;
#16017=CARTESIAN_POINT ( 'NONE',  ( -56.99451991528749062, 28.92564299267978001, 4.000000000000000000 ) ) ;
#16022=VERTEX_POINT ( 'NONE', #132055 ) ;
#16023=ORIENTED_EDGE ( 'NONE', *, *, #12577, .F. ) ;
#16024=VERTEX_POINT ( 'NONE', #32745 ) ;
#16025=DIRECTION ( 'NONE',  ( -0.7071067811865486830, -0.7071067811865464625, -0.000000000000000000 ) ) ;
#16026=ORIENTED_EDGE ( 'NONE', *, *, #75182, .F. ) ;
#16027=DIRECTION ( 'NONE',  ( 0.7071067811865487940, 0.7071067811865463515, 0.000000000000000000 ) ) ;
#16028=DIRECTION ( 'NONE',  ( 0.6830127018922181881, 0.6830127018922202975, -0.2588190451025214056 ) ) ;
#16029=DIRECTION ( 'NONE',  ( -0.6830127018922181881, 0.6830127018922202975, -0.2588190451025214056 ) ) ;
#16031=ORIENTED_EDGE ( 'NONE', *, *, #94382, .T. ) ;
#16034=CARTESIAN_POINT ( 'NONE',  ( 32.99451991528749062, 28.92564299267960948, 4.000000000000000000 ) ) ;
#16035=CARTESIAN_POINT ( 'NONE',  ( 1.500000000000001332, 4.087461875839200509, 4.000000000000000000 ) ) ;
#16036=CARTESIAN_POINT ( 'NONE',  ( 56.99451991528749062, 28.92564299267978001, 4.000000000000000000 ) ) ;
#16037=PLANE ( 'NONE',  #126432 ) ;
#16040=EDGE_CURVE ( 'NONE', #113241, #96641, #10933, .T. ) ;
#16042=ORIENTED_EDGE ( 'NONE', *, *, #129738, .T. ) ;
#16043=ORIENTED_EDGE ( 'NONE', *, *, #123732, .F. ) ;
#16045=ORIENTED_EDGE ( 'NONE', *, *, #1162, .F. ) ;
#16046=VERTEX_POINT ( 'NONE', #125454 ) ;
#16047=PLANE ( 'NONE',  #90008 ) ;
#16048=DIRECTION ( 'NONE',  ( -0.6830127018922181881, 0.6830127018922202975, -0.2588190451025214056 ) ) ;
#16049=ORIENTED_EDGE ( 'NONE', *, *, #44502, .F. ) ;
#16050=DIRECTION ( 'NONE',  ( -1.000000000000000000, 0.000000000000000000, 0.000000000000000000 ) ) ;
#16054=ORIENTED_EDGE ( 'NONE', *, *, #50542, .T. ) ;
#16055=DIRECTION ( 'NONE',  ( 0.6830127018922180770, -0.6830127018922204085, -0.2588190451025213501 ) ) ;
#16056=VERTEX_POINT ( 'NONE', #47917 ) ;
#16057=CARTESIAN_POINT ( 'NONE',  ( 48.18398860626899705, 28.73617430169820608, 5.000000000000000000 ) ) ;
#16058=VECTOR ( 'NONE', #9551, 1000.000000000000000 ) ;
#16059=VECTOR ( 'NONE', #134617, 1000.000000000000000 ) ;
#16060=AXIS2_PLACEMENT_3D ( 'NONE', #78432, #67579, #24750 ) ;
#16061=CARTESIAN_POINT ( 'NONE',  ( -17.01088028653936490, -22.02621442084248216, 4.990779571109221990 ) ) ;
#16062=CARTESIAN_POINT ( 'NONE',  ( -15.18398860626900237, 28.73617430169797871, 5.000000000000000000 ) ) ;
#16063=VECTOR ( 'NONE', #105622, 1000.000000000000000 ) ;
#16064=FACE_OUTER_BOUND ( 'NONE', #28336, .T. ) ;
#16065=ORIENTED_EDGE ( 'NONE', *, *, #86789, .T. ) ;
#16066=ORIENTED_EDGE ( 'NONE', *, *, #13430, .F. ) ;
#16067=CARTESIAN_POINT ( 'NONE',  ( 0.000000000000000000, 0.000000000000000000, 5.000000000000000000 ) ) ;
#16068=CARTESIAN_POINT ( 'NONE',  ( -38.39513766812456197, 21.75929247661549226, 21.32995629748195299 ) ) ;
#16069=DIRECTION ( 'NONE',  ( -0.7071067811865487940, 0.7071067811865463515, -0.000000000000000000 ) ) ;
#16070=CARTESIAN_POINT ( 'NONE',  ( -10.49999999999992184, -16.53360074219757081, 5.000000000000000000 ) ) ;
#16072=VECTOR ( 'NONE', #80423, 1000.000000000000227 ) ;
#16074=ORIENTED_EDGE ( 'NONE', *, *, #103559, .F. ) ;
#16076=DIRECTION ( 'NONE',  ( -0.000000000000000000, 0.000000000000000000, 1.000000000000000000 ) ) ;
#16077=ORIENTED_EDGE ( 'NONE', *, *, #135002, .T. ) ;
#16078=VERTEX_POINT ( 'NONE', #61643 ) ;
#16079=VECTOR ( 'NONE', #54272, 1000.000000000000227 ) ;
#16080=CARTESIAN_POINT ( 'NONE',  ( 0.000000000000000000, 0.000000000000000000, 5.000000000000000000 ) ) ;
#16081=VERTEX_POINT ( 'NONE', #71087 ) ;
#16082=( BOUNDED_CURVE ( )  B_SPLINE_CURVE ( 3, ( #2632, #45478, #101965, #89655 ),
 .UNSPECIFIED., .F., .F. ) 
 B_SPLINE_CURVE_WITH_KNOTS ( ( 4, 4 ),
 ( 1.502886732431669481, 1.547827028402603444 ),
 .UNSPECIFIED. ) 
 CURVE ( )  GEOMETRIC_REPRESENTATION_ITEM ( )  RATIONAL_B_SPLINE_CURVE ( ( 1.000000000000000000, 0.9998317045644854462, 0.9998317045644854462, 1.000000000000000000 ) ) 
 REPRESENTATION_ITEM ( '' )  );
#16083=VECTOR ( 'NONE', #68028, 1000.000000000000000 ) ;
#16084=LINE ( 'NONE', #38604, #74285 ) ;
#16085=EDGE_LOOP ( 'NONE', ( #96094, #142214, #32431, #95338 ) ) ;
#16087=EDGE_CURVE ( 'NONE', #100461, #109420, #115231, .T. ) ;
#16088=CARTESIAN_POINT ( 'NONE',  ( -39.29974487139159578, -27.71228299555233576, 4.000000000000000000 ) ) ;
#16089=VECTOR ( 'NONE', #130049, 1000.000000000000227 ) ;
#16090=AXIS2_PLACEMENT_3D ( 'NONE', #95766, #137869, #5872 ) ;
#16092=AXIS2_PLACEMENT_3D ( 'NONE', #43350, #10676, #85396 ) ;
#16093=ADVANCED_FACE ( 'NONE', ( #126166 ), #126848, .F. ) ;
#16094=FACE_BOUND ( 'NONE', #102277, .T. ) ;
#16096=EDGE_CURVE ( 'NONE', #95958, #135598, #36302, .T. ) ;
#16098=VECTOR ( 'NONE', #1507, 999.9999999999998863 ) ;
#16099=CARTESIAN_POINT ( 'NONE',  ( -18.18398860626898994, 28.73617430169800002, 5.000000000000000000 ) ) ;
#16100=VERTEX_POINT ( 'NONE', #48601 ) ;
#16101=LINE ( 'NONE', #5939, #110572 ) ;
#16102=LINE ( 'NONE', #92993, #52915 ) ;
#16104=AXIS2_PLACEMENT_3D ( 'NONE', #82953, #81550, #51039 ) ;
#16105=DIRECTION ( 'NONE',  ( 0.7071067811865486830, -0.7071067811865464625, -0.000000000000000000 ) ) ;
#16106=EDGE_LOOP ( 'NONE', ( #54586, #56183, #38311 ) ) ;
#16107=EDGE_CURVE ( 'NONE', #70402, #27000, #135616, .T. ) ;
#16108=ADVANCED_FACE ( 'NONE', ( #27536 ), #137036, .F. ) ;
#16109=ORIENTED_EDGE ( 'NONE', *, *, #135904, .T. ) ;
#16111=EDGE_LOOP ( 'NONE', ( #137898, #121790, #22098, #116284 ) ) ;
#16112=DIRECTION ( 'NONE',  ( 0.7071067811865487940, 0.7071067811865463515, 0.000000000000000000 ) ) ;
#16113=LINE ( 'NONE', #12034, #42702 ) ;
#16115=ORIENTED_EDGE ( 'NONE', *, *, #20089, .T. ) ;
#16119=EDGE_CURVE ( 'NONE', #92930, #39160, #82665, .T. ) ;
#16120=CARTESIAN_POINT ( 'NONE',  ( -20.99999999999984368, 8.816494571476647835, 4.604407763760409722 ) ) ;
#16121=CARTESIAN_POINT ( 'NONE',  ( 0.000000000000000000, 0.000000000000000000, 5.000000000000000000 ) ) ;
#16122=DIRECTION ( 'NONE',  ( 0.7071067811865487940, 0.7071067811865463515, 0.000000000000000000 ) ) ;
#16123=CARTESIAN_POINT ( 'NONE',  ( 31.82816939922330235, 12.75929247661557930, 4.000000000000000000 ) ) ;
#16125=EDGE_LOOP ( 'NONE', ( #62876, #23900, #108585, #114920 ) ) ;
#16126=ORIENTED_EDGE ( 'NONE', *, *, #23529, .F. ) ;
#16128=DIRECTION ( 'NONE',  ( 0.3543493200069162685, -0.000000000000000000, -0.9351131265310288487 ) ) ;
#16129=VERTEX_POINT ( 'NONE', #69669 ) ;
#16130=ADVANCED_FACE ( 'NONE', ( #113846 ), #138471, .F. ) ;
#16131=EDGE_LOOP ( 'NONE', ( #11174, #28695, #133507, #138448 ) ) ;
#16133=CARTESIAN_POINT ( 'NONE',  ( -51.29974487139158867, -27.71228299555242103, 4.000000000000000000 ) ) ;
#16135=DIRECTION ( 'NONE',  ( -1.000000000000000000, 1.242409592863268950E-14, 0.000000000000000000 ) ) ;
#16136=ORIENTED_EDGE ( 'NONE', *, *, #83954, .F. ) ;
#16137=DIRECTION ( 'NONE',  ( 0.3543493200069162685, -0.000000000000000000, -0.9351131265310288487 ) ) ;
#16138=EDGE_CURVE ( 'NONE', #96656, #71407, #75361, .T. ) ;
#16139=FACE_OUTER_BOUND ( 'NONE', #77895, .T. ) ;
#16141=DIRECTION ( 'NONE',  ( -0.7071067811865487940, 0.7071067811865463515, -0.000000000000000000 ) ) ;
#16142=VERTEX_POINT ( 'NONE', #120230 ) ;
#16143=DIRECTION ( 'NONE',  ( -0.7071067811865486830, -0.7071067811865464625, 0.000000000000000000 ) ) ;
#16144=FACE_OUTER_BOUND ( 'NONE', #104632, .T. ) ;
#16145=EDGE_CURVE ( 'NONE', #92724, #81113, #52162, .T. ) ;
#16146=CARTESIAN_POINT ( 'NONE',  ( -34.92500000000001137, 9.759292476615614831, 4.255531930566240462 ) ) ;
#16148=ORIENTED_EDGE ( 'NONE', *, *, #109856, .T. ) ;
#16149=CARTESIAN_POINT ( 'NONE',  ( 45.48921356237309510, -27.52281430457087197, 5.000000000000000000 ) ) ;
#16150=EDGE_LOOP ( 'NONE', ( #102820, #59770, #119214, #54096 ) ) ;
#16151=CARTESIAN_POINT ( 'NONE',  ( 14.99451991528749595, 28.92564299267948513, 4.000000000000000000 ) ) ;
#16152=DIRECTION ( 'NONE',  ( 0.3543493200069162685, -0.000000000000000000, -0.9351131265310288487 ) ) ;
#16153=ORIENTED_EDGE ( 'NONE', *, *, #36259, .T. ) ;
#16154=ADVANCED_FACE ( 'NONE', ( #52852 ), #119525, .F. ) ;
#16155=VECTOR ( 'NONE', #36172, 1000.000000000000227 ) ;
#16156=EDGE_CURVE ( 'NONE', #125554, #128057, #129003, .T. ) ;
#16157=CARTESIAN_POINT ( 'NONE',  ( -28.49999999999979394, -11.94781430457070392, 5.000000000000000000 ) ) ;
#16158=DIRECTION ( 'NONE',  ( -0.7071067811865486830, -0.7071067811865464625, -0.000000000000000000 ) ) ;
#16159=FACE_OUTER_BOUND ( 'NONE', #111935, .T. ) ;
#16160=ORIENTED_EDGE ( 'NONE', *, *, #19312, .F. ) ;
#16161=AXIS2_PLACEMENT_3D ( 'NONE', #27573, #16710, #59535 ) ;
#16164=PLANE ( 'NONE',  #115612 ) ;
#16165=LINE ( 'NONE', #103643, #60878 ) ;
#16166=EDGE_CURVE ( 'NONE', #32877, #22044, #18807, .T. ) ;
#16167=CARTESIAN_POINT ( 'NONE',  ( -20.99999999999985079, 12.83542986846995149, -1.025386466790322304 ) ) ;
#16168=EDGE_CURVE ( 'NONE', #13363, #42048, #41277, .T. ) ;
#16170=CARTESIAN_POINT ( 'NONE',  ( -33.48921356237309510, -27.52281430457078670, 5.000000000000000000 ) ) ;
#16172=VERTEX_POINT ( 'NONE', #62351 ) ;
#16175=AXIS2_PLACEMENT_3D ( 'NONE', #128749, #19280, #43190 ) ;
#16176=LINE ( 'NONE', #125710, #99189 ) ;
#16178=CARTESIAN_POINT ( 'NONE',  ( 34.92499999999998295, 19.44114312045510218, 6.054907437694465600 ) ) ;
#16179=DIRECTION ( 'NONE',  ( -0.7071067811865487940, 0.7071067811865463515, 0.000000000000000000 ) ) ;
#16180=CARTESIAN_POINT ( 'NONE',  ( 34.45011844616451668, -13.48371918836236638, 5.000000000000000000 ) ) ;
#16182=ORIENTED_EDGE ( 'NONE', *, *, #135695, .F. ) ;
#16184=DIRECTION ( 'NONE',  ( -0.6830127018922181881, 0.6830127018922202975, -0.2588190451025214056 ) ) ;
#16186=VECTOR ( 'NONE', #34990, 1000.000000000000000 ) ;
#16187=VECTOR ( 'NONE', #36072, 1000.000000000000000 ) ;
#16188=LINE ( 'NONE', #18323, #143245 ) ;
#16190=DIRECTION ( 'NONE',  ( 0.7071067811865487940, -0.7071067811865463515, 0.000000000000000000 ) ) ;
#16191=VECTOR ( 'NONE', #98815, 999.9999999999998863 ) ;
#16192=ORIENTED_EDGE ( 'NONE', *, *, #44118, .F. ) ;
#16193=EDGE_CURVE ( 'NONE', #111746, #10669, #29679, .T. ) ;
#16194=ORIENTED_EDGE ( 'NONE', *, *, #124096, .T. ) ;
#16196=VERTEX_POINT ( 'NONE', #73919 ) ;
#16197=DIRECTION ( 'NONE',  ( -0.7071067811865486830, -0.7071067811865464625, 0.000000000000000000 ) ) ;
#16198=VECTOR ( 'NONE', #4235, 1000.000000000000000 ) ;
#16199=LINE ( 'NONE', #125735, #16473 ) ;
#16200=FACE_OUTER_BOUND ( 'NONE', #13619, .T. ) ;
#16201=EDGE_CURVE ( 'NONE', #54027, #116082, #118098, .T. ) ;
#16202=CARTESIAN_POINT ( 'NONE',  ( -57.48921356237308800, -27.52281430457095368, 5.000000000000000000 ) ) ;
#16204=VECTOR ( 'NONE', #49226, 1000.000000000000227 ) ;
#16205=ORIENTED_EDGE ( 'NONE', *, *, #130583, .F. ) ;
#16206=CARTESIAN_POINT ( 'NONE',  ( -2.999999999999978240, -8.731860332648842871, -2.120594902707545693 ) ) ;
#16207=DIRECTION ( 'NONE',  ( -0.7071067811865486830, -0.7071067811865464625, 0.000000000000000000 ) ) ;
#16209=CARTESIAN_POINT ( 'NONE',  ( 34.92499999999998295, -22.22500000000000142, 4.500000000000000888 ) ) ;
#16213=LINE ( 'NONE', #3898, #110780 ) ;
#16214=VECTOR ( 'NONE', #32194, 1000.000000000000000 ) ;
#16215=EDGE_LOOP ( 'NONE', ( #129024, #134222, #35659, #85921 ) ) ;
#16216=EDGE_LOOP ( 'NONE', ( #139615, #127709, #83449, #77657 ) ) ;
#16218=DIRECTION ( 'NONE',  ( -0.7071067811865486830, -0.7071067811865464625, 0.000000000000000000 ) ) ;
#16219=DIRECTION ( 'NONE',  ( 0.7071067811865487940, 0.7071067811865463515, 0.000000000000000000 ) ) ;
#16221=ORIENTED_EDGE ( 'NONE', *, *, #108591, .T. ) ;
#16222=EDGE_CURVE ( 'NONE', #46584, #98313, #18062, .T. ) ;
#16223=EDGE_CURVE ( 'NONE', #107048, #83184, #51466, .T. ) ;
#16226=DIRECTION ( 'NONE',  ( -0.6830127018922181881, 0.6830127018922202975, -0.2588190451025214056 ) ) ;
#16227=ORIENTED_EDGE ( 'NONE', *, *, #51792, .F. ) ;
#16229=VECTOR ( 'NONE', #88766, 1000.000000000000000 ) ;
#16230=CARTESIAN_POINT ( 'NONE',  ( -21.29974487139158512, -27.71228299555221142, 4.000000000000000000 ) ) ;
#16231=DIRECTION ( 'NONE',  ( 0.7071067811865487940, 0.7071067811865463515, 0.000000000000000000 ) ) ;
#16232=CARTESIAN_POINT ( 'NONE',  ( 18.52400138585436551, 22.03583458319438648, 4.979811245910089390 ) ) ;
#16233=DIRECTION ( 'NONE',  ( -1.000000000000000000, 0.000000000000000000, 0.000000000000000000 ) ) ;
#16234=EDGE_CURVE ( 'NONE', #68584, #90591, #86942, .T. ) ;
#16235=CARTESIAN_POINT ( 'NONE',  ( -28.36246187583881806, 22.22500000000000853, 4.000000000000000000 ) ) ;
#16238=CARTESIAN_POINT ( 'NONE',  ( -42.29974487139158157, -27.71228299555235708, 4.000000000000000000 ) ) ;
#16241=VECTOR ( 'NONE', #49788, 1000.000000000000000 ) ;
#16242=DIRECTION ( 'NONE',  ( 0.7071067811865487940, 0.7071067811865463515, 0.000000000000000000 ) ) ;
#16244=EDGE_LOOP ( 'NONE', ( #86637, #119742, #104921, #111558 ) ) ;
#16245=ORIENTED_EDGE ( 'NONE', *, *, #131670, .F. ) ;
#16246=( BOUNDED_CURVE ( )  B_SPLINE_CURVE ( 3, ( #36983, #92793, #125445, #37732 ),
 .UNSPECIFIED., .F., .T. ) 
 B_SPLINE_CURVE_WITH_KNOTS ( ( 4, 4 ),
 ( 1.864375635226959815, 1.933014472006526763 ),
 .UNSPECIFIED. ) 
 CURVE ( )  GEOMETRIC_REPRESENTATION_ITEM ( )  RATIONAL_B_SPLINE_CURVE ( ( 1.000000000000000000, 0.9996074310407769836, 0.9996074310407769836, 1.000000000000000000 ) ) 
 REPRESENTATION_ITEM ( '' )  );
#16247=LINE ( 'NONE', #127180, #122887 ) ;
#16248=CARTESIAN_POINT ( 'NONE',  ( -8.999999999999932498, 8.966399257802164513, 5.000000000000000000 ) ) ;
#16249=CARTESIAN_POINT ( 'NONE',  ( 54.18398860626899705, 28.73617430169825226, 5.000000000000000000 ) ) ;
#16250=ORIENTED_EDGE ( 'NONE', *, *, #49554, .T. ) ;
#16251=ORIENTED_EDGE ( 'NONE', *, *, #52673, .F. ) ;
#16252=DIRECTION ( 'NONE',  ( 0.7071067811865487940, -0.7071067811865463515, 0.000000000000000000 ) ) ;
#16253=VECTOR ( 'NONE', #23705, 999.9999999999998863 ) ;
#16254=ORIENTED_EDGE ( 'NONE', *, *, #66618, .F. ) ;
#16255=VECTOR ( 'NONE', #85479, 1000.000000000000114 ) ;
#16259=ORIENTED_EDGE ( 'NONE', *, *, #21008, .F. ) ;
#16260=ADVANCED_FACE ( 'NONE', ( #89096 ), #89777, .F. ) ;
#16261=LINE ( 'NONE', #104735, #122064 ) ;
#16262=CARTESIAN_POINT ( 'NONE',  ( 32.99999999999977973, 12.25461709320624060, -10.07315571508689622 ) ) ;
#16264=AXIS2_PLACEMENT_3D ( 'NONE', #102359, #26908, #137833 ) ;
#16266=VECTOR ( 'NONE', #52353, 999.9999999999998863 ) ;
#16267=FACE_BOUND ( 'NONE', #115775, .T. ) ;
#16268=DIRECTION ( 'NONE',  ( -0.7071067811865487940, 0.7071067811865463515, -0.000000000000000000 ) ) ;
#16269=EDGE_CURVE ( 'NONE', #116931, #32517, #77517, .T. ) ;
#16270=FACE_OUTER_BOUND ( 'NONE', #48268, .T. ) ;
#16271=LINE ( 'NONE', #53021, #129301 ) ;
#16272=VECTOR ( 'NONE', #97158, 1000.000000000000000 ) ;
#16273=DIRECTION ( 'NONE',  ( 0.7071067811865487940, 0.7071067811865463515, -0.000000000000000000 ) ) ;
#16274=VERTEX_POINT ( 'NONE', #134020 ) ;
#16276=CARTESIAN_POINT ( 'NONE',  ( 2.700255128608413990, -27.71228299555204089, 4.000000000000000000 ) ) ;
#16278=ORIENTED_EDGE ( 'NONE', *, *, #84434, .F. ) ;
#16279=EDGE_CURVE ( 'NONE', #26178, #53860, #35452, .T. ) ;
#16280=ADVANCED_FACE ( 'NONE', ( #66624 ), #34709, .T. ) ;
#16281=ORIENTED_EDGE ( 'NONE', *, *, #24647, .T. ) ;
#16283=ORIENTED_EDGE ( 'NONE', *, *, #75771, .F. ) ;
#16284=EDGE_CURVE ( 'NONE', #43072, #93569, #122402, .T. ) ;
#16285=DIRECTION ( 'NONE',  ( 1.000000000000000000, 0.000000000000000000, 0.000000000000000000 ) ) ;
#16287=DIRECTION ( 'NONE',  ( 0.6830127018922181881, 0.6830127018922202975, -0.2588190451025214056 ) ) ;
#16288=EDGE_CURVE ( 'NONE', #100222, #46561, #79686, .T. ) ;
#16289=VECTOR ( 'NONE', #22327, 1000.000000000000000 ) ;
#16290=LINE ( 'NONE', #132261, #116611 ) ;
#16291=VERTEX_POINT ( 'NONE', #121680 ) ;
#16292=CARTESIAN_POINT ( 'NONE',  ( -34.92500000000001137, -11.14387692260744522, 4.000000000000000000 ) ) ;
#16293=ADVANCED_FACE ( 'NONE', ( #76808 ), #88384, .F. ) ;
#16294=VECTOR ( 'NONE', #27021, 1000.000000000000114 ) ;
#16295=CARTESIAN_POINT ( 'NONE',  ( -32.99451991528749062, 28.92564299267960948, 4.000000000000000000 ) ) ;
#16297=DIRECTION ( 'NONE',  ( -0.3543493200069162685, -0.000000000000000000, -0.9351131265310288487 ) ) ;
#16298=LINE ( 'NONE', #8788, #1812 ) ;
#16299=PLANE ( 'NONE',  #126060 ) ;
#16300=DIRECTION ( 'NONE',  ( -0.7071067811865486830, -0.7071067811865464625, 0.000000000000000000 ) ) ;
#16302=CARTESIAN_POINT ( 'NONE',  ( -72.48921356237309510, -27.52281430457106026, 5.000000000000000000 ) ) ;
#16303=ORIENTED_EDGE ( 'NONE', *, *, #117790, .F. ) ;
#16304=VECTOR ( 'NONE', #51729, 1000.000000000000000 ) ;
#16305=CARTESIAN_POINT ( 'NONE',  ( -29.99999999999979039, 10.21212019023806583, -2.019456568337728797 ) ) ;
#16306=CARTESIAN_POINT ( 'NONE',  ( -26.67183060077628198, -3.740707523384238176, 4.000000000000000000 ) ) ;
#16308=ORIENTED_EDGE ( 'NONE', *, *, #92951, .T. ) ;
#16309=VERTEX_POINT ( 'NONE', #67346 ) ;
#16310=EDGE_CURVE ( 'NONE', #74842, #81201, #619, .T. ) ;
#16312=ORIENTED_EDGE ( 'NONE', *, *, #67751, .T. ) ;
#16315=EDGE_CURVE ( 'NONE', #109570, #80973, #101374, .T. ) ;
#16316=VECTOR ( 'NONE', #106059, 1000.000000000000000 ) ;
#16319=ORIENTED_EDGE ( 'NONE', *, *, #4330, .F. ) ;
#16320=EDGE_LOOP ( 'NONE', ( #91059, #20724, #140019, #68855 ) ) ;
#16321=VECTOR ( 'NONE', #126106, 1000.000000000000000 ) ;
#16323=CARTESIAN_POINT ( 'NONE',  ( -5.510786437626906675, -27.52281430457051314, 5.000000000000000000 ) ) ;
#16324=ORIENTED_EDGE ( 'NONE', *, *, #109642, .T. ) ;
#16325=ORIENTED_EDGE ( 'NONE', *, *, #36160, .T. ) ;
#16326=CARTESIAN_POINT ( 'NONE',  ( -34.92500000000001137, -12.28150956279563566, 4.759050581649337808 ) ) ;
#16329=DIRECTION ( 'NONE',  ( -0.7071067811865487940, 0.7071067811865463515, 0.000000000000000000 ) ) ;
#16330=ORIENTED_EDGE ( 'NONE', *, *, #12967, .T. ) ;
#16331=ORIENTED_EDGE ( 'NONE', *, *, #67741, .F. ) ;
#16332=EDGE_LOOP ( 'NONE', ( #52948, #128127, #71049, #118794 ) ) ;
#16333=ORIENTED_EDGE ( 'NONE', *, *, #130466, .T. ) ;
#16335=DIRECTION ( 'NONE',  ( -0.7071067811865486830, -0.7071067811865464625, 0.000000000000000000 ) ) ;
#16336=AXIS2_PLACEMENT_3D ( 'NONE', #5803, #59538, #115266 ) ;
#16337=CARTESIAN_POINT ( 'NONE',  ( 80.99451991528748351, 28.92564299267994699, 4.000000000000000000 ) ) ;
#16340=DIRECTION ( 'NONE',  ( -0.7071067811865486830, -0.7071067811865464625, 0.000000000000000000 ) ) ;
#16341=ORIENTED_EDGE ( 'NONE', *, *, #7805, .F. ) ;
#16343=VECTOR ( 'NONE', #8661, 1000.000000000000000 ) ;
#16344=DIRECTION ( 'NONE',  ( 0.7071067811865487940, 0.7071067811865463515, 0.000000000000000000 ) ) ;
#16345=EDGE_CURVE ( 'NONE', #58222, #92260, #142745, .T. ) ;
#16347=CARTESIAN_POINT ( 'NONE',  ( 11.99999999999993072, 14.58746187583909837, 4.000000000000000000 ) ) ;
#16348=CARTESIAN_POINT ( 'NONE',  ( 51.18398860626899705, 28.73617430169823095, 5.000000000000000000 ) ) ;
#16349=DIRECTION ( 'NONE',  ( 0.7071067811865487940, 0.7071067811865463515, 0.000000000000000000 ) ) ;
#16350=EDGE_LOOP ( 'NONE', ( #70177, #64311, #116014, #69493 ) ) ;
#16351=ORIENTED_EDGE ( 'NONE', *, *, #75961, .F. ) ;
#16352=EDGE_CURVE ( 'NONE', #35346, #125640, #94590, .T. ) ;
#16353=EDGE_LOOP ( 'NONE', ( #98324, #81762, #90608, #67492, #58893 ) ) ;
#16354=DIRECTION ( 'NONE',  ( 0.7071067811865487940, -0.7071067811865463515, 0.000000000000000000 ) ) ;
#16355=CARTESIAN_POINT ( 'NONE',  ( -39.48921356237310221, -27.52281430457082934, 5.000000000000000000 ) ) ;
#16356=CARTESIAN_POINT ( 'NONE',  ( 29.99999999999979039, -9.033600742197645417, 5.000000000000000000 ) ) ;
#16357=DIRECTION ( 'NONE',  ( 1.000000000000000000, 0.000000000000000000, 0.000000000000000000 ) ) ;
#16359=DIRECTION ( 'NONE',  ( 0.7071067811865487940, 0.7071067811865463515, 0.000000000000000000 ) ) ;
#16362=VECTOR ( 'NONE', #31815, 1000.000000000000000 ) ;
#16364=DIRECTION ( 'NONE',  ( -0.7071067811865487940, 0.7071067811865463515, -0.000000000000000000 ) ) ;
#16365=EDGE_CURVE ( 'NONE', #10400, #29217, #72193, .T. ) ;
#16366=FACE_OUTER_BOUND ( 'NONE', #105724, .T. ) ;
#16367=CARTESIAN_POINT ( 'NONE',  ( -17.00492477221184018, -5.240707523384225297, 12.38332538355500034 ) ) ;
#16368=VERTEX_POINT ( 'NONE', #73579 ) ;
#16369=VECTOR ( 'NONE', #106758, 1000.000000000000227 ) ;
#16371=VECTOR ( 'NONE', #32277, 1000.000000000000000 ) ;
#16372=VECTOR ( 'NONE', #98646, 1000.000000000000000 ) ;
#16374=ORIENTED_EDGE ( 'NONE', *, *, #142804, .F. ) ;
#16375=AXIS2_PLACEMENT_3D ( 'NONE', #83045, #8296, #85889 ) ;
#16377=LINE ( 'NONE', #5507, #95035 ) ;
#16378=ORIENTED_EDGE ( 'NONE', *, *, #53551, .F. ) ;
#16380=FACE_OUTER_BOUND ( 'NONE', #27704, .T. ) ;
#16382=ORIENTED_EDGE ( 'NONE', *, *, #50180, .F. ) ;
#16383=DIRECTION ( 'NONE',  ( -0.7071067811865487940, 0.7071067811865463515, -0.000000000000000000 ) ) ;
#16384=ORIENTED_EDGE ( 'NONE', *, *, #113382, .F. ) ;
#16385=PLANE ( 'NONE',  #139381 ) ;
#16386=VECTOR ( 'NONE', #138956, 1000.000000000000000 ) ;
#16388=FACE_OUTER_BOUND ( 'NONE', #57684, .T. ) ;
#16391=VERTEX_POINT ( 'NONE', #84473 ) ;
#16393=CARTESIAN_POINT ( 'NONE',  ( 19.49999999999986500, -8.568876922607721269, 4.000000000000000000 ) ) ;
#16394=CARTESIAN_POINT ( 'NONE',  ( -34.92500000000001137, 3.207916084809872448, -2.206283991393058752 ) ) ;
#16397=VECTOR ( 'NONE', #91135, 1000.000000000000000 ) ;
#16399=VERTEX_POINT ( 'NONE', #128666 ) ;
#16400=AXIS2_PLACEMENT_3D ( 'NONE', #85654, #95828, #130636 ) ;
#16401=CARTESIAN_POINT ( 'NONE',  ( -39.18398860626899705, 28.73617430169814568, 5.000000000000000000 ) ) ;
#16402=VERTEX_POINT ( 'NONE', #61322 ) ;
#16403=VECTOR ( 'NONE', #13227, 1000.000000000000000 ) ;
#16404=EDGE_CURVE ( 'NONE', #58311, #18399, #17729, .T. ) ;
#16406=VECTOR ( 'NONE', #142752, 1000.000000000000000 ) ;
#16407=LINE ( 'NONE', #115703, #142629 ) ;
#16408=CARTESIAN_POINT ( 'NONE',  ( 12.83652871126541939, 15.75929247661555976, 9.299976744542947316 ) ) ;
#16409=DIRECTION ( 'NONE',  ( 0.7071067811865486830, -0.7071067811865464625, -0.000000000000000000 ) ) ;
#16410=ORIENTED_EDGE ( 'NONE', *, *, #19301, .F. ) ;
#16414=LINE ( 'NONE', #107013, #122592 ) ;
#16416=EDGE_CURVE ( 'NONE', #124216, #107217, #29336, .T. ) ;
#16417=LINE ( 'NONE', #59969, #105026 ) ;
#16418=DIRECTION ( 'NONE',  ( 0.3543493200069162685, -0.000000000000000000, -0.9351131265310288487 ) ) ;
#16419=ORIENTED_EDGE ( 'NONE', *, *, #97526, .T. ) ;
#16420=DIRECTION ( 'NONE',  ( -0.7071067811865487940, 0.7071067811865463515, 0.000000000000000000 ) ) ;
#16421=CARTESIAN_POINT ( 'NONE',  ( 11.20710678118646797, -11.24070752338417378, 5.000000000000000000 ) ) ;
#16424=EDGE_LOOP ( 'NONE', ( #16535, #125986, #125436, #14880 ) ) ;
#16425=ORIENTED_EDGE ( 'NONE', *, *, #54035, .T. ) ;
#16426=VERTEX_POINT ( 'NONE', #116363 ) ;
#16428=ORIENTED_EDGE ( 'NONE', *, *, #41196, .T. ) ;
#16429=CARTESIAN_POINT ( 'NONE',  ( -6.183988606268994381, 28.73617430169791476, 5.000000000000000000 ) ) ;
#16430=CARTESIAN_POINT ( 'NONE',  ( -23.89661266223020419, -0.3091507863911187037, 4.000000000000000000 ) ) ;
#16431=AXIS2_PLACEMENT_3D ( 'NONE', #107719, #77286, #19992 ) ;
#16433=CARTESIAN_POINT ( 'NONE',  ( 5.510786437626906675, -27.52281430457051314, 5.000000000000000000 ) ) ;
#16434=ORIENTED_EDGE ( 'NONE', *, *, #18342, .T. ) ;
#16435=VECTOR ( 'NONE', #19420, 999.9999999999998863 ) ;
#16436=EDGE_CURVE ( 'NONE', #29394, #36181, #117749, .T. ) ;
#16437=FACE_OUTER_BOUND ( 'NONE', #51919, .T. ) ;
#16438=CARTESIAN_POINT ( 'NONE',  ( -10.49999999999991829, 13.56627193232213813, -10.57019076586071193 ) ) ;
#16439=ORIENTED_EDGE ( 'NONE', *, *, #51908, .F. ) ;
#16440=DIRECTION ( 'NONE',  ( -0.7071067811865487940, 0.7071067811865463515, 0.000000000000000000 ) ) ;
#16441=CARTESIAN_POINT ( 'NONE',  ( -11.67183060077638146, -9.740707523384180888, 4.000000000000000000 ) ) ;
#16442=PLANE ( 'NONE',  #5262 ) ;
#16443=VECTOR ( 'NONE', #129410, 999.9999999999998863 ) ;
#16444=ORIENTED_EDGE ( 'NONE', *, *, #90558, .T. ) ;
#16445=ORIENTED_EDGE ( 'NONE', *, *, #16234, .T. ) ;
#16446=DIRECTION ( 'NONE',  ( 0.7071067811865487940, 0.7071067811865463515, -0.000000000000000000 ) ) ;
#16447=DIRECTION ( 'NONE',  ( 0.000000000000000000, 1.000000000000000000, 0.000000000000000000 ) ) ;
#16448=DIRECTION ( 'NONE',  ( 0.7071067811865487940, 0.7071067811865463515, 0.000000000000000000 ) ) ;
#16451=VECTOR ( 'NONE', #39087, 999.9999999999998863 ) ;
#16452=CARTESIAN_POINT ( 'NONE',  ( -66.48921356237309510, -27.52281430457101763, 5.000000000000000000 ) ) ;
#16455=ORIENTED_EDGE ( 'NONE', *, *, #73788, .T. ) ;
#16456=ADVANCED_FACE ( 'NONE', ( #60596 ), #50403, .F. ) ;
#16457=VERTEX_POINT ( 'NONE', #96024 ) ;
#16458=ORIENTED_EDGE ( 'NONE', *, *, #42892, .F. ) ;
#16459=ADVANCED_FACE ( 'NONE', ( #106898 ), #104768, .F. ) ;
#16460=ORIENTED_EDGE ( 'NONE', *, *, #120562, .T. ) ;
#16461=EDGE_CURVE ( 'NONE', #60720, #13220, #82323, .T. ) ;
#16462=VECTOR ( 'NONE', #68989, 1000.000000000000000 ) ;
#16463=ADVANCED_FACE ( 'NONE', ( #138842 ), #106163, .F. ) ;
#16464=DIRECTION ( 'NONE',  ( 0.3543493200069162685, -0.000000000000000000, -0.9351131265310288487 ) ) ;
#16465=VECTOR ( 'NONE', #96181, 1000.000000000000000 ) ;
#16466=VECTOR ( 'NONE', #25206, 1000.000000000000227 ) ;
#16467=EDGE_LOOP ( 'NONE', ( #22153, #109919, #26630, #42364 ) ) ;
#16470=FACE_OUTER_BOUND ( 'NONE', #70218, .T. ) ;
#16471=CARTESIAN_POINT ( 'NONE',  ( -16.49999999999988987, -5.568876922607749691, 4.000000000000000000 ) ) ;
#16472=VECTOR ( 'NONE', #137654, 1000.000000000000000 ) ;
#16473=VECTOR ( 'NONE', #139489, 1000.000000000000000 ) ;
#16474=AXIS2_PLACEMENT_3D ( 'NONE', #59412, #103571, #94124 ) ;
#16475=VECTOR ( 'NONE', #10037, 1000.000000000000000 ) ;
#16476=LINE ( 'NONE', #50561, #21300 ) ;
#16477=EDGE_LOOP ( 'NONE', ( #64431, #31443, #28427, #24586 ) ) ;
#16479=PLANE ( 'NONE',  #109640 ) ;
#16480=DIRECTION ( 'NONE',  ( -1.000000000000000000, 2.840831291283848700E-14, 0.000000000000000000 ) ) ;
#16481=ADVANCED_FACE ( 'NONE', ( #71441 ), #93886, .T. ) ;
#16483=DIRECTION ( 'NONE',  ( 0.6830127018922181881, 0.6830127018922202975, -0.2588190451025214056 ) ) ;
#16485=EDGE_CURVE ( 'NONE', #69167, #61103, #41646, .T. ) ;
#16486=EDGE_LOOP ( 'NONE', ( #88154, #43526, #74983, #9155 ) ) ;
#16487=DIRECTION ( 'NONE',  ( 1.000000000000000000, 0.000000000000000000, 0.000000000000000000 ) ) ;
#16488=VERTEX_POINT ( 'NONE', #76443 ) ;
#16489=ORIENTED_EDGE ( 'NONE', *, *, #71975, .T. ) ;
#16494=DIRECTION ( 'NONE',  ( -0.7071067811865486830, -0.7071067811865464625, 0.000000000000000000 ) ) ;
#16495=CARTESIAN_POINT ( 'NONE',  ( 1.362461875839014791, 22.22500000000000142, 4.000000000000000000 ) ) ;
#16496=PLANE ( 'NONE',  #10221 ) ;
#16498=LINE ( 'NONE', #107090, #86559 ) ;
#16499=AXIS2_PLACEMENT_3D ( 'NONE', #63761, #1138, #8589 ) ;
#16500=LINE ( 'NONE', #85330, #14291 ) ;
#16502=EDGE_CURVE ( 'NONE', #142939, #109568, #53991, .T. ) ;
#16503=FACE_OUTER_BOUND ( 'NONE', #79379, .T. ) ;
#16505=LINE ( 'NONE', #71641, #95342 ) ;
#16506=VECTOR ( 'NONE', #128307, 1000.000000000000000 ) ;
#16508=VERTEX_POINT ( 'NONE', #130104 ) ;
#16509=VECTOR ( 'NONE', #48384, 1000.000000000000000 ) ;
#16510=PLANE ( 'NONE',  #124451 ) ;
#16511=DIRECTION ( 'NONE',  ( 0.7071067811865487940, -0.7071067811865463515, 0.000000000000000000 ) ) ;
#16512=ORIENTED_EDGE ( 'NONE', *, *, #143197, .F. ) ;
#16514=ORIENTED_EDGE ( 'NONE', *, *, #97551, .T. ) ;
#16515=EDGE_CURVE ( 'NONE', #114036, #35724, #143108, .T. ) ;
#16517=VERTEX_POINT ( 'NONE', #119893 ) ;
#16518=VECTOR ( 'NONE', #64386, 1000.000000000000000 ) ;
#16519=DIRECTION ( 'NONE',  ( -0.7071067811865486830, 0.7071067811865464625, 0.000000000000000000 ) ) ;
#16521=VECTOR ( 'NONE', #124810, 1000.000000000000000 ) ;
#16522=CARTESIAN_POINT ( 'NONE',  ( 4.499999999999968914, -20.56887692260760048, 4.000000000000000000 ) ) ;
#16523=LINE ( 'NONE', #4168, #94924 ) ;
#16524=ORIENTED_EDGE ( 'NONE', *, *, #10811, .T. ) ;
#16525=DIRECTION ( 'NONE',  ( 0.7071067811865486830, -0.7071067811865464625, -0.000000000000000000 ) ) ;
#16526=ORIENTED_EDGE ( 'NONE', *, *, #89079, .T. ) ;
#16527=EDGE_CURVE ( 'NONE', #86631, #27690, #8966, .T. ) ;
#16529=CARTESIAN_POINT ( 'NONE',  ( 9.299744871391588674, -27.71228299555212971, 4.000000000000000000 ) ) ;
#16530=CARTESIAN_POINT ( 'NONE',  ( -17.99451991528748351, 28.92564299267950645, 4.000000000000000000 ) ) ;
#16532=VERTEX_POINT ( 'NONE', #98871 ) ;
#16533=VERTEX_POINT ( 'NONE', #87308 ) ;
#16534=VECTOR ( 'NONE', #33771, 1000.000000000000000 ) ;
#16535=ORIENTED_EDGE ( 'NONE', *, *, #61205, .F. ) ;
#16536=DIRECTION ( 'NONE',  ( -0.000000000000000000, -0.3543493200069152693, 0.9351131265310292928 ) ) ;
#16537=CARTESIAN_POINT ( 'NONE',  ( 0.04658813629544733548, 14.25929247661557753, 18.84478104361328121 ) ) ;
#16538=DIRECTION ( 'NONE',  ( -0.7071067811865486830, -0.7071067811865464625, 0.000000000000000000 ) ) ;
#16539=VECTOR ( 'NONE', #43512, 1000.000000000000000 ) ;
#16541=DIRECTION ( 'NONE',  ( 0.7071067811865487940, 0.7071067811865463515, -0.000000000000000000 ) ) ;
#16542=FACE_OUTER_BOUND ( 'NONE', #40123, .T. ) ;
#16543=CARTESIAN_POINT ( 'NONE',  ( -21.70701326429289324, -21.74070752338406010, 4.999753212805221558 ) ) ;
#16544=EDGE_CURVE ( 'NONE', #35109, #118679, #32957, .T. ) ;
#16545=DIRECTION ( 'NONE',  ( -0.6830127018922180770, -0.6830127018922204085, -0.2588190451025213501 ) ) ;
#16546=CARTESIAN_POINT ( 'NONE',  ( 36.18398860626899705, 28.73617430169812437, 5.000000000000000000 ) ) ;
#16547=VECTOR ( 'NONE', #126694, 999.9999999999998863 ) ;
#16549=DIRECTION ( 'NONE',  ( -0.7071067811865487940, 0.7071067811865463515, 0.000000000000000000 ) ) ;
#16551=CARTESIAN_POINT ( 'NONE',  ( 31.49999999999979039, -20.56887692260760758, 4.000000000000000000 ) ) ;
#16552=ORIENTED_EDGE ( 'NONE', *, *, #137954, .T. ) ;
#16553=( BOUNDED_CURVE ( )  B_SPLINE_CURVE ( 3, ( #107045, #6256, #29475, #73711 ),
 .UNSPECIFIED., .F., .T. ) 
 B_SPLINE_CURVE_WITH_KNOTS ( ( 4, 4 ),
 ( 5.390251506879594423, 5.422326034329065791 ),
 .UNSPECIFIED. ) 
 CURVE ( )  GEOMETRIC_REPRESENTATION_ITEM ( )  RATIONAL_B_SPLINE_CURVE ( ( 1.000000000000000000, 0.9999142705615216009, 0.9999142705615216009, 1.000000000000000000 ) ) 
 REPRESENTATION_ITEM ( '' )  );
#16554=PLANE ( 'NONE',  #64572 ) ;
#16555=CARTESIAN_POINT ( 'NONE',  ( 4.499999999999979572, 0.05218569542916884352, 5.000000000000000000 ) ) ;
#16556=ORIENTED_EDGE ( 'NONE', *, *, #127960, .F. ) ;
#16557=EDGE_CURVE ( 'NONE', #79734, #2427, #133993, .T. ) ;
#16558=CARTESIAN_POINT ( 'NONE',  ( 9.299744871391588674, -27.71228299555212971, 4.000000000000000000 ) ) ;
#16559=CARTESIAN_POINT ( 'NONE',  ( 28.98012225071434855, -17.24070752338409562, 20.23474786156475957 ) ) ;
#16560=VECTOR ( 'NONE', #18152, 1000.000000000000000 ) ;
#16561=VERTEX_POINT ( 'NONE', #99575 ) ;
#16562=FACE_OUTER_BOUND ( 'NONE', #112810, .T. ) ;
#16564=DIRECTION ( 'NONE',  ( 0.6830127018922180770, -0.6830127018922204085, -0.2588190451025213501 ) ) ;
#16565=CARTESIAN_POINT ( 'NONE',  ( -7.968364840778035862, 2.259292476615690770, 13.77329220150635614 ) ) ;
#16567=CARTESIAN_POINT ( 'NONE',  ( -2.816011393730999401, 28.73617430169785436, 5.000000000000000000 ) ) ;
#16568=CARTESIAN_POINT ( 'NONE',  ( -34.06996025486387936, -0.7407075233842770334, 13.87443053587618813 ) ) ;
#16569=CARTESIAN_POINT ( 'NONE',  ( 72.18398860626899705, 28.73617430169837661, 5.000000000000000000 ) ) ;
#16570=ADVANCED_FACE ( 'NONE', ( #77174 ), #130836, .T. ) ;
#16571=PLANE ( 'NONE',  #142066 ) ;
#16572=LINE ( 'NONE', #4953, #69254 ) ;
#16575=CARTESIAN_POINT ( 'NONE',  ( 42.48921356237308800, -27.52281430457085065, 5.000000000000000000 ) ) ;
#16578=FACE_OUTER_BOUND ( 'NONE', #70948, .T. ) ;
#16580=ORIENTED_EDGE ( 'NONE', *, *, #29567, .F. ) ;
#16581=VERTEX_POINT ( 'NONE', #110451 ) ;
#16582=AXIS2_PLACEMENT_3D ( 'NONE', #87847, #45105, #119729 ) ;
#16584=AXIS2_PLACEMENT_3D ( 'NONE', #97594, #52669, #143255 ) ;
#16586=ORIENTED_EDGE ( 'NONE', *, *, #76601, .T. ) ;
#16587=EDGE_LOOP ( 'NONE', ( #70812, #124823, #109180, #66812 ) ) ;
#16588=ADVANCED_FACE ( 'NONE', ( #109763 ), #11125, .F. ) ;
#16589=CARTESIAN_POINT ( 'NONE',  ( 11.29298673570687050, -21.74070752338406365, 4.999753212805220670 ) ) ;
#16590=CARTESIAN_POINT ( 'NONE',  ( -66.48921356237309510, -27.52281430457101763, 5.000000000000000000 ) ) ;
#16592=VECTOR ( 'NONE', #97731, 1000.000000000000000 ) ;
#16595=DIRECTION ( 'NONE',  ( 0.7071067811865487940, 0.7071067811865463515, 0.000000000000000000 ) ) ;
#16596=VERTEX_POINT ( 'NONE', #55403 ) ;
#16597=LINE ( 'NONE', #105044, #115743 ) ;
#16598=VECTOR ( 'NONE', #118887, 1000.000000000000000 ) ;
#16599=CARTESIAN_POINT ( 'NONE',  ( 15.48921356237309510, -27.52281430457066236, 5.000000000000000000 ) ) ;
#16600=CARTESIAN_POINT ( 'NONE',  ( 19.49999999999986144, 9.127013188829479873, 4.802533355213541633 ) ) ;
#16601=PLANE ( 'NONE',  #14194 ) ;
#16603=ADVANCED_FACE ( 'NONE', ( #42397 ), #98185, .F. ) ;
#16604=DIRECTION ( 'NONE',  ( 0.6830127018922180770, -0.6830127018922204085, -0.2588190451025213501 ) ) ;
#16605=FACE_OUTER_BOUND ( 'NONE', #23660, .T. ) ;
#16606=AXIS2_PLACEMENT_3D ( 'NONE', #16062, #135753, #4440 ) ;
#16607=DIRECTION ( 'NONE',  ( 1.000000000000000000, 0.000000000000000000, 0.000000000000000000 ) ) ;
#16609=DIRECTION ( 'NONE',  ( 0.6830127018922180770, -0.6830127018922204085, -0.2588190451025213501 ) ) ;
#16610=DIRECTION ( 'NONE',  ( 0.7071067811865487940, -0.7071067811865463515, 0.000000000000000000 ) ) ;
#16611=DIRECTION ( 'NONE',  ( -0.7071067811865486830, 0.7071067811865464625, 0.000000000000000000 ) ) ;
#16612=DIRECTION ( 'NONE',  ( -0.6830127018922180770, -0.6830127018922204085, -0.2588190451025213501 ) ) ;
#16613=VERTEX_POINT ( 'NONE', #88751 ) ;
#16614=EDGE_LOOP ( 'NONE', ( #26368, #107621, #60034, #13121 ) ) ;
#16618=LINE ( 'NONE', #118045, #29247 ) ;
#16619=ORIENTED_EDGE ( 'NONE', *, *, #114876, .F. ) ;
#16620=EDGE_CURVE ( 'NONE', #33358, #61647, #142414, .T. ) ;
#16621=DIRECTION ( 'NONE',  ( 0.7071067811865487940, 0.7071067811865463515, 0.000000000000000000 ) ) ;
#16622=FACE_OUTER_BOUND ( 'NONE', #125276, .T. ) ;
#16623=AXIS2_PLACEMENT_3D ( 'NONE', #28820, #74480, #15731 ) ;
#16624=VECTOR ( 'NONE', #7545, 1000.000000000000000 ) ;
#16626=VERTEX_POINT ( 'NONE', #118489 ) ;
#16627=AXIS2_PLACEMENT_3D ( 'NONE', #57948, #49198, #137623 ) ;
#16628=ORIENTED_EDGE ( 'NONE', *, *, #133031, .T. ) ;
#16629=CARTESIAN_POINT ( 'NONE',  ( 8.218373117074998291, 21.74787736706806385, 4.999607392498049308 ) ) ;
#16630=LINE ( 'NONE', #118054, #16777 ) ;
#16631=AXIS2_PLACEMENT_3D ( 'NONE', #28753, #60699, #61416 ) ;
#16632=CARTESIAN_POINT ( 'NONE',  ( -2.816011393730999401, 28.73617430169785436, 5.000000000000000000 ) ) ;
#16634=VERTEX_POINT ( 'NONE', #19189 ) ;
#16635=ORIENTED_EDGE ( 'NONE', *, *, #14998, .T. ) ;
#16636=ORIENTED_EDGE ( 'NONE', *, *, #103835, .T. ) ;
#16637=LINE ( 'NONE', #5745, #90824 ) ;
#16638=DIRECTION ( 'NONE',  ( 0.7071067811865487940, 0.7071067811865463515, 0.000000000000000000 ) ) ;
#16640=VECTOR ( 'NONE', #127211, 1000.000000000000000 ) ;
#16641=PLANE ( 'NONE',  #71082 ) ;
#16642=EDGE_CURVE ( 'NONE', #140124, #100866, #19884, .T. ) ;
#16644=EDGE_CURVE ( 'NONE', #91814, #94048, #86607, .T. ) ;
#16646=ORIENTED_EDGE ( 'NONE', *, *, #123562, .F. ) ;
#16647=VERTEX_POINT ( 'NONE', #46715 ) ;
#16648=EDGE_CURVE ( 'NONE', #61464, #107040, #101743, .T. ) ;
#16649=DIRECTION ( 'NONE',  ( -0.6830127018922181881, 0.6830127018922202975, -0.2588190451025214056 ) ) ;
#16650=VERTEX_POINT ( 'NONE', #135125 ) ;
#16651=ORIENTED_EDGE ( 'NONE', *, *, #72838, .T. ) ;
#16652=VECTOR ( 'NONE', #10726, 1000.000000000000227 ) ;
#16653=VECTOR ( 'NONE', #66534, 999.9999999999998863 ) ;
#16654=EDGE_CURVE ( 'NONE', #38177, #80628, #47423, .T. ) ;
#16655=ADVANCED_FACE ( 'NONE', ( #111924 ), #59013, .F. ) ;
#16657=DIRECTION ( 'NONE',  ( 4.681814790819592407E-17, 0.3543493200069153248, 0.9351131265310292928 ) ) ;
#16658=DIRECTION ( 'NONE',  ( -0.6830127018922181881, 0.6830127018922202975, -0.2588190451025214056 ) ) ;
#16659=ORIENTED_EDGE ( 'NONE', *, *, #65767, .F. ) ;
#16660=FACE_OUTER_BOUND ( 'NONE', #8044, .T. ) ;
#16661=DIRECTION ( 'NONE',  ( -0.000000000000000000, 0.3543493200069153248, 0.9351131265310292928 ) ) ;
#16662=VECTOR ( 'NONE', #53403, 1000.000000000000000 ) ;
#16663=CARTESIAN_POINT ( 'NONE',  ( -24.29974487139158867, -27.71228299555223273, 4.000000000000000000 ) ) ;
#16664=CARTESIAN_POINT ( 'NONE',  ( 28.49999999999980815, 7.466399257802192935, 5.000000000000000000 ) ) ;
#16665=ORIENTED_EDGE ( 'NONE', *, *, #99609, .F. ) ;
#16666=CARTESIAN_POINT ( 'NONE',  ( -19.83957586139685247, 9.091547215995101183, 4.000000000000000000 ) ) ;
#16667=FACE_BOUND ( 'NONE', #137643, .T. ) ;
#16668=EDGE_CURVE ( 'NONE', #109897, #31681, #80730, .T. ) ;
#16669=EDGE_LOOP ( 'NONE', ( #42187, #66573, #110058, #127474 ) ) ;
#16670=CARTESIAN_POINT ( 'NONE',  ( 15.04658813629535707, 14.25929247661557042, 18.84478104361324213 ) ) ;
#16671=LINE ( 'NONE', #62350, #98993 ) ;
#16672=ADVANCED_FACE ( 'NONE', ( #114045 ), #124922, .F. ) ;
#16673=ORIENTED_EDGE ( 'NONE', *, *, #72761, .T. ) ;
#16674=PLANE ( 'NONE',  #52731 ) ;
#16675=ORIENTED_EDGE ( 'NONE', *, *, #125511, .T. ) ;
#16676=ORIENTED_EDGE ( 'NONE', *, *, #76213, .T. ) ;
#16679=VERTEX_POINT ( 'NONE', #68445 ) ;
#16680=( BOUNDED_CURVE ( )  B_SPLINE_CURVE ( 3, ( #70833, #125917, #114981, #126594 ),
 .UNSPECIFIED., .F., .T. ) 
 B_SPLINE_CURVE_WITH_KNOTS ( ( 4, 4 ),
 ( 5.920967161967927161, 7.341195215986594746 ),
 .UNSPECIFIED. ) 
 CURVE ( )  GEOMETRIC_REPRESENTATION_ITEM ( )  RATIONAL_B_SPLINE_CURVE ( ( 1.000000000000000000, 0.8388583629366707095, 0.8388583629366707095, 1.000000000000000000 ) ) 
 REPRESENTATION_ITEM ( '' )  );
#16681=EDGE_CURVE ( 'NONE', #106218, #24833, #13997, .T. ) ;
#16682=DIRECTION ( 'NONE',  ( -0.000000000000000000, -0.3543493200069152693, 0.9351131265310292928 ) ) ;
#16683=DIRECTION ( 'NONE',  ( 1.000000000000000000, 0.000000000000000000, 0.000000000000000000 ) ) ;
#16684=DIRECTION ( 'NONE',  ( -0.7071067811865487940, 0.7071067811865463515, -0.000000000000000000 ) ) ;
#16685=DIRECTION ( 'NONE',  ( 1.000000000000000000, 0.000000000000000000, 0.000000000000000000 ) ) ;
#16688=ADVANCED_FACE ( 'NONE', ( #77859 ), #90896, .F. ) ;
#16689=AXIS2_PLACEMENT_3D ( 'NONE', #77212, #67781, #56192 ) ;
#16690=AXIS2_PLACEMENT_3D ( 'NONE', #43405, #120203, #20913 ) ;
#16691=LINE ( 'NONE', #27550, #53806 ) ;
#16692=VECTOR ( 'NONE', #131726, 1000.000000000000227 ) ;
#16693=VECTOR ( 'NONE', #38613, 1000.000000000000000 ) ;
#16694=DIRECTION ( 'NONE',  ( -0.7071067811865486830, -0.7071067811865464625, 0.000000000000000000 ) ) ;
#16696=LINE ( 'NONE', #5072, #52923 ) ;
#16697=CARTESIAN_POINT ( 'NONE',  ( -24.48921356237309510, -27.52281430457072631, 5.000000000000000000 ) ) ;
#16699=ORIENTED_EDGE ( 'NONE', *, *, #92350, .T. ) ;
#16700=VECTOR ( 'NONE', #24449, 1000.000000000000000 ) ;
#16701=EDGE_CURVE ( 'NONE', #52797, #33791, #133670, .T. ) ;
#16704=VERTEX_POINT ( 'NONE', #91586 ) ;
#16705=DIRECTION ( 'NONE',  ( -0.6830127018922181881, 0.6830127018922202975, -0.2588190451025214056 ) ) ;
#16706=ORIENTED_EDGE ( 'NONE', *, *, #139666, .F. ) ;
#16707=EDGE_LOOP ( 'NONE', ( #104002, #45864, #837, #115052 ) ) ;
#16708=CARTESIAN_POINT ( 'NONE',  ( -34.42500000000001137, 21.72500000000000142, 5.000000000000000000 ) ) ;
#16709=CARTESIAN_POINT ( 'NONE',  ( 25.17183060077629619, 9.759292476615618384, 4.000000000000000000 ) ) ;
#16710=DIRECTION ( 'NONE',  ( 0.6830127018922180770, -0.6830127018922204085, -0.2588190451025213501 ) ) ;
#16711=EDGE_CURVE ( 'NONE', #105009, #81280, #122048, .T. ) ;
#16712=ORIENTED_EDGE ( 'NONE', *, *, #93579, .F. ) ;
#16713=EDGE_CURVE ( 'NONE', #50240, #43657, #14735, .T. ) ;
#16714=CARTESIAN_POINT ( 'NONE',  ( 0.000000000000000000, 0.000000000000000000, 5.000000000000000000 ) ) ;
#16716=PLANE ( 'NONE',  #141621 ) ;
#16717=EDGE_CURVE ( 'NONE', #71266, #102417, #124212, .T. ) ;
#16719=ORIENTED_EDGE ( 'NONE', *, *, #134644, .T. ) ;
#16721=CARTESIAN_POINT ( 'NONE',  ( -51.48921356237309510, -27.52281430457091460, 5.000000000000000000 ) ) ;
#16723=CARTESIAN_POINT ( 'NONE',  ( -9.792893218813382816, -11.24070752338416845, 5.000000000000000000 ) ) ;
#16724=ORIENTED_EDGE ( 'NONE', *, *, #113199, .T. ) ;
#16725=EDGE_LOOP ( 'NONE', ( #33648, #107515, #51869, #106268 ) ) ;
#16726=FACE_OUTER_BOUND ( 'NONE', #39668, .T. ) ;
#16727=ORIENTED_EDGE ( 'NONE', *, *, #83958, .F. ) ;
#16729=CARTESIAN_POINT ( 'NONE',  ( -17.99999999999987566, -10.77435723561697145, -9.972017380717186796 ) ) ;
#16730=CARTESIAN_POINT ( 'NONE',  ( -60.18398860626900415, 28.73617430169829490, 5.000000000000000000 ) ) ;
#16731=EDGE_CURVE ( 'NONE', #113815, #107142, #113316, .T. ) ;
#16734=ORIENTED_EDGE ( 'NONE', *, *, #18210, .T. ) ;
#16735=AXIS2_PLACEMENT_3D ( 'NONE', #107949, #73240, #119545 ) ;
#16736=PLANE ( 'NONE',  #18227 ) ;
#16737=VECTOR ( 'NONE', #30091, 1000.000000000000000 ) ;
#16738=DIRECTION ( 'NONE',  ( -0.7071067811865486830, -0.7071067811865464625, 0.000000000000000000 ) ) ;
#16739=DIRECTION ( 'NONE',  ( 0.3543493200069162685, -0.000000000000000000, -0.9351131265310288487 ) ) ;
#16740=ORIENTED_EDGE ( 'NONE', *, *, #21739, .F. ) ;
#16742=AXIS2_PLACEMENT_3D ( 'NONE', #110208, #23949, #132736 ) ;
#16743=CARTESIAN_POINT ( 'NONE',  ( 16.49999999999988987, 13.08746187583910370, 4.000000000000000000 ) ) ;
#16744=VERTEX_POINT ( 'NONE', #89436 ) ;
#16745=PLANE ( 'NONE',  #2294 ) ;
#16746=VERTEX_POINT ( 'NONE', #112623 ) ;
#16747=VERTEX_POINT ( 'NONE', #36491 ) ;
#16749=DIRECTION ( 'NONE',  ( 0.3543493200069162685, -0.000000000000000000, -0.9351131265310288487 ) ) ;
#16752=CARTESIAN_POINT ( 'NONE',  ( -4.499999999999968914, 7.466399257802187606, 5.000000000000000000 ) ) ;
#16753=( BOUNDED_CURVE ( )  B_SPLINE_CURVE ( 3, ( #41531, #119792, #29942, #7473 ),
 .UNSPECIFIED., .F., .T. ) 
 B_SPLINE_CURVE_WITH_KNOTS ( ( 4, 4 ),
 ( 5.043186909253416950, 5.074607125596347856 ),
 .UNSPECIFIED. ) 
 CURVE ( )  GEOMETRIC_REPRESENTATION_ITEM ( )  RATIONAL_B_SPLINE_CURVE ( ( 1.000000000000000000, 0.9999177325257868620, 0.9999177325257868620, 1.000000000000000000 ) ) 
 REPRESENTATION_ITEM ( '' )  );
#16754=CARTESIAN_POINT ( 'NONE',  ( 24.48921356237309510, -27.52281430457072631, 5.000000000000000000 ) ) ;
#16755=DIRECTION ( 'NONE',  ( 0.7071067811865486830, 0.7071067811865463515, 0.000000000000000000 ) ) ;
#16756=ORIENTED_EDGE ( 'NONE', *, *, #115986, .T. ) ;
#16757=CARTESIAN_POINT ( 'NONE',  ( -2.999999999999971578, -4.447814304570786526, 5.000000000000000000 ) ) ;
#16758=LINE ( 'NONE', #6544, #46621 ) ;
#16760=DIRECTION ( 'NONE',  ( 0.3543493200069162685, -0.000000000000000000, -0.9351131265310288487 ) ) ;
#16763=DIRECTION ( 'NONE',  ( 0.7071067811865487940, 0.7071067811865463515, -0.000000000000000000 ) ) ;
#16764=DIRECTION ( 'NONE',  ( -0.7071067811865486830, -0.7071067811865464625, 0.000000000000000000 ) ) ;
#16765=CARTESIAN_POINT ( 'NONE',  ( 21.18398860626899349, 28.73617430169802134, 5.000000000000000000 ) ) ;
#16766=LINE ( 'NONE', #115320, #106656 ) ;
#16767=CARTESIAN_POINT ( 'NONE',  ( 32.20710678118632586, -8.240707523384191546, 5.000000000000000000 ) ) ;
#16768=ORIENTED_EDGE ( 'NONE', *, *, #17417, .F. ) ;
#16769=ORIENTED_EDGE ( 'NONE', *, *, #80517, .T. ) ;
#16770=ORIENTED_EDGE ( 'NONE', *, *, #75371, .F. ) ;
#16772=ORIENTED_EDGE ( 'NONE', *, *, #44181, .F. ) ;
#16773=ORIENTED_EDGE ( 'NONE', *, *, #28086, .T. ) ;
#16774=VERTEX_POINT ( 'NONE', #983 ) ;
#16775=CARTESIAN_POINT ( 'NONE',  ( 2.700255128608413990, -27.71228299555204089, 4.000000000000000000 ) ) ;
#16776=LINE ( 'NONE', #103759, #134316 ) ;
#16777=VECTOR ( 'NONE', #39118, 999.9999999999998863 ) ;
#16778=ORIENTED_EDGE ( 'NONE', *, *, #109942, .F. ) ;
#16779=DIRECTION ( 'NONE',  ( 0.6830127018922180770, -0.6830127018922204085, -0.2588190451025213501 ) ) ;
#16780=DIRECTION ( 'NONE',  ( 0.7071067811865487940, 0.7071067811865463515, 0.000000000000000000 ) ) ;
#16781=DIRECTION ( 'NONE',  ( -0.3543493200069162685, -0.000000000000000000, -0.9351131265310288487 ) ) ;
#16782=CARTESIAN_POINT ( 'NONE',  ( 72.18398860626899705, 28.73617430169837661, 5.000000000000000000 ) ) ;
#16785=VERTEX_POINT ( 'NONE', #2396 ) ;
#16786=LINE ( 'NONE', #49459, #104265 ) ;
#16787=LINE ( 'NONE', #96453, #86376 ) ;
#16789=LINE ( 'NONE', #72656, #79695 ) ;
#16790=AXIS2_PLACEMENT_3D ( 'NONE', #139324, #61071, #40013 ) ;
#16791=LINE ( 'NONE', #116814, #16929 ) ;
#16792=LINE ( 'NONE', #117505, #84524 ) ;
#16794=PLANE ( 'NONE',  #80124 ) ;
#16795=ADVANCED_FACE ( 'NONE', ( #136502 ), #138673, .T. ) ;
#16798=ORIENTED_EDGE ( 'NONE', *, *, #45064, .F. ) ;
#16799=ORIENTED_EDGE ( 'NONE', *, *, #135953, .F. ) ;
#16801=VERTEX_POINT ( 'NONE', #104597 ) ;
#16802=EDGE_CURVE ( 'NONE', #140847, #4302, #83583, .T. ) ;
#16804=CARTESIAN_POINT ( 'NONE',  ( 23.89661266223020419, -0.3091507863911187037, 4.000000000000000000 ) ) ;
#16805=EDGE_LOOP ( 'NONE', ( #66834, #102036, #92760, #19762 ) ) ;
#16807=VECTOR ( 'NONE', #43665, 1000.000000000000000 ) ;
#16808=VECTOR ( 'NONE', #107586, 1000.000000000000227 ) ;
#16810=DIRECTION ( 'NONE',  ( 1.000000000000000000, 0.000000000000000000, 0.000000000000000000 ) ) ;
#16811=AXIS2_PLACEMENT_3D ( 'NONE', #142441, #106190, #109063 ) ;
#16812=EDGE_CURVE ( 'NONE', #127177, #133750, #18263, .T. ) ;
#16813=DIRECTION ( 'NONE',  ( 0.6830127018922180770, -0.6830127018922204085, -0.2588190451025213501 ) ) ;
#16814=CARTESIAN_POINT ( 'NONE',  ( 53.99451991528749062, 28.92564299267975869, 4.000000000000000000 ) ) ;
#16815=VECTOR ( 'NONE', #112270, 1000.000000000000227 ) ;
#16818=CARTESIAN_POINT ( 'NONE',  ( 60.29974487139158867, -27.71228299555248142, 4.000000000000000000 ) ) ;
#16820=AXIS2_PLACEMENT_3D ( 'NONE', #125595, #128442, #37876 ) ;
#16822=PLANE ( 'NONE',  #95892 ) ;
#16823=ADVANCED_FACE ( 'NONE', ( #17569 ), #81454, .T. ) ;
#16824=CARTESIAN_POINT ( 'NONE',  ( 5.994519915287488843, 28.92564299267942118, 4.000000000000000000 ) ) ;
#16825=FACE_OUTER_BOUND ( 'NONE', #128059, .T. ) ;
#16827=ORIENTED_EDGE ( 'NONE', *, *, #49078, .T. ) ;
#16829=ORIENTED_EDGE ( 'NONE', *, *, #88004, .T. ) ;
#16830=DIRECTION ( 'NONE',  ( -0.7071067811865486830, -0.7071067811865464625, 0.000000000000000000 ) ) ;
#16831=DIRECTION ( 'NONE',  ( 0.3543493200069163240, 0.000000000000000000, 0.9351131265310288487 ) ) ;
#16832=DIRECTION ( 'NONE',  ( -0.000000000000000000, 0.3543493200069153248, 0.9351131265310292928 ) ) ;
#16834=PLANE ( 'NONE',  #60312 ) ;
#16835=EDGE_CURVE ( 'NONE', #54369, #84048, #117577, .T. ) ;
#16836=VECTOR ( 'NONE', #33021, 1000.000000000000000 ) ;
#16838=ORIENTED_EDGE ( 'NONE', *, *, #90982, .F. ) ;
#16840=EDGE_CURVE ( 'NONE', #84066, #50105, #72008, .T. ) ;
#16841=CARTESIAN_POINT ( 'NONE',  ( 23.99999999999984013, 16.55218569542900298, 5.000000000000000000 ) ) ;
#16843=ORIENTED_EDGE ( 'NONE', *, *, #64343, .F. ) ;
#16844=DIRECTION ( 'NONE',  ( -0.000000000000000000, 0.3543493200069153248, 0.9351131265310291818 ) ) ;
#16845=ORIENTED_EDGE ( 'NONE', *, *, #58621, .F. ) ;
#16846=VECTOR ( 'NONE', #96362, 999.9999999999998863 ) ;
#16847=EDGE_CURVE ( 'NONE', #123433, #91250, #28486, .T. ) ;
#16848=EDGE_CURVE ( 'NONE', #112433, #89628, #62540, .T. ) ;
#16850=DIRECTION ( 'NONE',  ( -0.3543493200069163240, -0.000000000000000000, -0.9351131265310288487 ) ) ;
#16851=ORIENTED_EDGE ( 'NONE', *, *, #68849, .T. ) ;
#16852=AXIS2_PLACEMENT_3D ( 'NONE', #72056, #128544, #138716 ) ;
#16854=DIRECTION ( 'NONE',  ( -0.000000000000000000, -0.3543493200069152693, 0.9351131265310292928 ) ) ;
#16855=VECTOR ( 'NONE', #46268, 1000.000000000000000 ) ;
#16856=EDGE_CURVE ( 'NONE', #122361, #34748, #106710, .T. ) ;
#16857=CARTESIAN_POINT ( 'NONE',  ( -12.70612307739187052, 22.22500000000000142, 4.000000000000000000 ) ) ;
#16858=FACE_BOUND ( 'NONE', #89617, .T. ) ;
#16860=LINE ( 'NONE', #26310, #105879 ) ;
#16862=DIRECTION ( 'NONE',  ( -0.000000000000000000, 0.3543493200069153248, 0.9351131265310292928 ) ) ;
#16863=VERTEX_POINT ( 'NONE', #16123 ) ;
#16865=CARTESIAN_POINT ( 'NONE',  ( 54.29974487139159578, -27.71228299555243879, 4.000000000000000000 ) ) ;
#16866=VERTEX_POINT ( 'NONE', #61833 ) ;
#16867=VERTEX_POINT ( 'NONE', #93013 ) ;
#16868=ORIENTED_EDGE ( 'NONE', *, *, #137292, .T. ) ;
#16871=ORIENTED_EDGE ( 'NONE', *, *, #63698, .F. ) ;
#16872=EDGE_CURVE ( 'NONE', #26872, #123892, #7403, .T. ) ;
#16873=DIRECTION ( 'NONE',  ( -0.7071067811865486830, 0.7071067811865464625, 0.000000000000000000 ) ) ;
#16874=CARTESIAN_POINT ( 'NONE',  ( 0.1839886062690032631, 28.73617430169787568, 5.000000000000000000 ) ) ;
#16875=VECTOR ( 'NONE', #113478, 1000.000000000000000 ) ;
#16876=ORIENTED_EDGE ( 'NONE', *, *, #46481, .F. ) ;
#16877=CARTESIAN_POINT ( 'NONE',  ( 20.67183060077633172, -9.740707523384180888, 4.000000000000000000 ) ) ;
#16878=VECTOR ( 'NONE', #123972, 1000.000000000000000 ) ;
#16879=ADVANCED_FACE ( 'NONE', ( #5260 ), #105993, .F. ) ;
#16880=CARTESIAN_POINT ( 'NONE',  ( -21.11237052021067129, 8.776708805967446736, 4.202873650309270737 ) ) ;
#16881=DIRECTION ( 'NONE',  ( 0.6830127018922181881, 0.6830127018922202975, -0.2588190451025214056 ) ) ;
#16882=LINE ( 'NONE', #38634, #38889 ) ;
#16884=LINE ( 'NONE', #27032, #18440 ) ;
#16887=EDGE_LOOP ( 'NONE', ( #141916, #134552, #19702, #62075 ) ) ;
#16888=CARTESIAN_POINT ( 'NONE',  ( -39.18398860626899705, 28.73617430169814568, 5.000000000000000000 ) ) ;
#16889=CARTESIAN_POINT ( 'NONE',  ( -3.005480084712505828, 28.92564299267936079, 4.000000000000000000 ) ) ;
#16890=ORIENTED_EDGE ( 'NONE', *, *, #80680, .T. ) ;
#16891=ORIENTED_EDGE ( 'NONE', *, *, #13550, .T. ) ;
#16892=EDGE_LOOP ( 'NONE', ( #130109, #111616, #108534 ) ) ;
#16895=VECTOR ( 'NONE', #35390, 1000.000000000000000 ) ;
#16896=VERTEX_POINT ( 'NONE', #6660 ) ;
#16897=CARTESIAN_POINT ( 'NONE',  ( 13.78501580275802141, -3.740707523384238176, 15.76143240460127082 ) ) ;
#16898=EDGE_CURVE ( 'NONE', #122922, #66605, #139407, .T. ) ;
#16901=LINE ( 'NONE', #105323, #70445 ) ;
#16902=EDGE_LOOP ( 'NONE', ( #82366, #87529, #11725, #112782 ) ) ;
#16903=DIRECTION ( 'NONE',  ( 0.6830127018922180770, 0.6830127018922202975, -0.2588190451025213501 ) ) ;
#16904=DIRECTION ( 'NONE',  ( 1.000000000000000000, 0.000000000000000000, 0.000000000000000000 ) ) ;
#16905=AXIS2_PLACEMENT_3D ( 'NONE', #10144, #100033, #103558 ) ;
#16906=DIRECTION ( 'NONE',  ( -0.7071067811865486830, -0.7071067811865464625, -0.000000000000000000 ) ) ;
#16907=ORIENTED_EDGE ( 'NONE', *, *, #19396, .T. ) ;
#16908=CARTESIAN_POINT ( 'NONE',  ( -26.99999999999980815, 11.96639925780214675, 5.000000000000000000 ) ) ;
#16909=ORIENTED_EDGE ( 'NONE', *, *, #83294, .T. ) ;
#16910=LINE ( 'NONE', #16151, #35743 ) ;
#16911=DIRECTION ( 'NONE',  ( 0.7071067811865487940, 0.7071067811865463515, 0.000000000000000000 ) ) ;
#16912=VECTOR ( 'NONE', #126217, 1000.000000000000000 ) ;
#16913=DIRECTION ( 'NONE',  ( -0.000000000000000000, 0.000000000000000000, 1.000000000000000000 ) ) ;
#16914=AXIS2_PLACEMENT_3D ( 'NONE', #138119, #38807, #85866 ) ;
#16915=EDGE_LOOP ( 'NONE', ( #27482, #113616, #102670, #51257 ) ) ;
#16916=LINE ( 'NONE', #125693, #28698 ) ;
#16917=DIRECTION ( 'NONE',  ( -0.7071067811865486830, 0.7071067811865464625, 0.000000000000000000 ) ) ;
#16918=CARTESIAN_POINT ( 'NONE',  ( -21.48921356237309155, -27.52281430457070499, 5.000000000000000000 ) ) ;
#16919=VECTOR ( 'NONE', #28149, 1000.000000000000000 ) ;
#16920=VERTEX_POINT ( 'NONE', #40784 ) ;
#16922=DIRECTION ( 'NONE',  ( 0.3543493200069162685, -0.000000000000000000, -0.9351131265310288487 ) ) ;
#16923=FACE_OUTER_BOUND ( 'NONE', #63620, .T. ) ;
#16924=DIRECTION ( 'NONE',  ( 0.3543493200069162685, -0.000000000000000000, -0.9351131265310288487 ) ) ;
#16925=CARTESIAN_POINT ( 'NONE',  ( -22.37177410554622980, -1.784312229707115893, 4.000000000000000000 ) ) ;
#16926=CARTESIAN_POINT ( 'NONE',  ( -35.18650864602339112, -15.74070752338412049, 8.904080028139022218 ) ) ;
#16927=ORIENTED_EDGE ( 'NONE', *, *, #70877, .F. ) ;
#16928=VERTEX_POINT ( 'NONE', #42933 ) ;
#16929=VECTOR ( 'NONE', #44283, 1000.000000000000000 ) ;
#16930=PLANE ( 'NONE',  #93526 ) ;
#16931=DIRECTION ( 'NONE',  ( 0.6830127018922180770, -0.6830127018922204085, -0.2588190451025213501 ) ) ;
#16933=CARTESIAN_POINT ( 'NONE',  ( 23.99451991528749062, 28.92564299267954908, 4.000000000000000000 ) ) ;
#16936=CARTESIAN_POINT ( 'NONE',  ( -28.78678096696623356, 12.75929247661558996, 10.29404684609028742 ) ) ;
#16937=CARTESIAN_POINT ( 'NONE',  ( -36.18398860626899705, 28.73617430169812437, 5.000000000000000000 ) ) ;
#16938=VERTEX_POINT ( 'NONE', #42220 ) ;
#16939=CARTESIAN_POINT ( 'NONE',  ( -63.48921356237309510, -27.52281430457099631, 5.000000000000000000 ) ) ;
#16940=ADVANCED_FACE ( 'NONE', ( #43615 ), #87840, .F. ) ;
#16941=FACE_OUTER_BOUND ( 'NONE', #77364, .T. ) ;
#16942=FACE_OUTER_BOUND ( 'NONE', #47157, .T. ) ;
#16945=VECTOR ( 'NONE', #130132, 999.9999999999998863 ) ;
#16948=EDGE_CURVE ( 'NONE', #34094, #105119, #19718, .T. ) ;
#16949=FACE_OUTER_BOUND ( 'NONE', #85502, .T. ) ;
#16951=ORIENTED_EDGE ( 'NONE', *, *, #32919, .T. ) ;
#16952=VERTEX_POINT ( 'NONE', #21865 ) ;
#16953=LINE ( 'NONE', #140167, #29312 ) ;
#16956=VECTOR ( 'NONE', #49749, 1000.000000000000227 ) ;
#16957=EDGE_CURVE ( 'NONE', #13692, #111562, #30629, .T. ) ;
#16958=CARTESIAN_POINT ( 'NONE',  ( -42.18398860626899705, 28.73617430169816700, 5.000000000000000000 ) ) ;
#16959=PLANE ( 'NONE',  #67313 ) ;
#16961=ADVANCED_FACE ( 'NONE', ( #32033 ), #77001, .F. ) ;
#16962=ORIENTED_EDGE ( 'NONE', *, *, #42728, .F. ) ;
#16963=DIRECTION ( 'NONE',  ( 0.7071067811865487940, 0.7071067811865463515, 0.000000000000000000 ) ) ;
#16964=CARTESIAN_POINT ( 'NONE',  ( 7.499999999999947597, -16.53360074219757081, 5.000000000000000000 ) ) ;
#16966=DIRECTION ( 'NONE',  ( 0.6830127018922181881, 0.6830127018922202975, -0.2588190451025214056 ) ) ;
#16968=CARTESIAN_POINT ( 'NONE',  ( -3.328169399223508851, 17.25929247661553489, 4.000000000000000000 ) ) ;
#16969=VECTOR ( 'NONE', #131225, 1000.000000000000000 ) ;
#16970=EDGE_CURVE ( 'NONE', #72338, #31169, #85682, .T. ) ;
#16972=ADVANCED_FACE ( 'NONE', ( #130659 ), #75549, .F. ) ;
#16973=DIRECTION ( 'NONE',  ( -0.000000000000000000, 0.000000000000000000, 1.000000000000000000 ) ) ;
#16974=ORIENTED_EDGE ( 'NONE', *, *, #24336, .T. ) ;
#16975=ORIENTED_EDGE ( 'NONE', *, *, #31824, .F. ) ;
#16977=CARTESIAN_POINT ( 'NONE',  ( -24.70710678118637560, 11.25929247661560417, 5.000000000000000000 ) ) ;
#16978=EDGE_CURVE ( 'NONE', #115946, #46130, #109588, .T. ) ;
#16979=LINE ( 'NONE', #136598, #57886 ) ;
#16980=VECTOR ( 'NONE', #80476, 1000.000000000000000 ) ;
#16982=( BOUNDED_CURVE ( )  B_SPLINE_CURVE ( 3, ( #53419, #8440, #7752, #56143 ),
 .UNSPECIFIED., .F., .F. ) 
 B_SPLINE_CURVE_WITH_KNOTS ( ( 4, 4 ),
 ( 2.779374508378134045, 4.199602562396851368 ),
 .UNSPECIFIED. ) 
 CURVE ( )  GEOMETRIC_REPRESENTATION_ITEM ( )  RATIONAL_B_SPLINE_CURVE ( ( 1.000000000000000000, 0.8388583629366599403, 0.8388583629366599403, 1.000000000000000000 ) ) 
 REPRESENTATION_ITEM ( '' )  );
#16984=EDGE_CURVE ( 'NONE', #16056, #110777, #52352, .T. ) ;
#16985=LINE ( 'NONE', #38039, #125353 ) ;
#16987=DIRECTION ( 'NONE',  ( 0.7071067811865486830, -0.7071067811865464625, -0.000000000000000000 ) ) ;
#16988=ORIENTED_EDGE ( 'NONE', *, *, #6146, .T. ) ;
#16989=ORIENTED_EDGE ( 'NONE', *, *, #52192, .T. ) ;
#16991=DIRECTION ( 'NONE',  ( -0.7071067811865486830, -0.7071067811865464625, 0.000000000000000000 ) ) ;
#16992=DIRECTION ( 'NONE',  ( 0.7071067811865487940, 0.7071067811865463515, 0.000000000000000000 ) ) ;
#16993=CARTESIAN_POINT ( 'NONE',  ( 18.79333936457835108, 21.75929247661549937, 4.998822639870708073 ) ) ;
#16995=LINE ( 'NONE', #72132, #62711 ) ;
#16997=ORIENTED_EDGE ( 'NONE', *, *, #87866, .F. ) ;
#16998=DIRECTION ( 'NONE',  ( -0.7071067811865487940, 0.7071067811865463515, -0.000000000000000000 ) ) ;
#16999=PLANE ( 'NONE',  #54639 ) ;
#17001=LINE ( 'NONE', #103974, #118813 ) ;
#17003=CARTESIAN_POINT ( 'NONE',  ( 15.29974487139158867, -27.71228299555216879, 4.000000000000000000 ) ) ;
#17005=ORIENTED_EDGE ( 'NONE', *, *, #93848, .T. ) ;
#17010=CARTESIAN_POINT ( 'NONE',  ( 33.29974487139158867, -27.71228299555229313, 4.000000000000000000 ) ) ;
#17011=DIRECTION ( 'NONE',  ( -0.000000000000000000, 0.3543493200069153248, 0.9351131265310292928 ) ) ;
#17012=VERTEX_POINT ( 'NONE', #32771 ) ;
#17013=ORIENTED_EDGE ( 'NONE', *, *, #117489, .F. ) ;
#17014=DIRECTION ( 'NONE',  ( 0.6830127018922181881, 0.6830127018922202975, -0.2588190451025214056 ) ) ;
#17015=CARTESIAN_POINT ( 'NONE',  ( 63.29974487139158867, -27.71228299555250274, 4.000000000000000000 ) ) ;
#17016=ORIENTED_EDGE ( 'NONE', *, *, #143326, .T. ) ;
#17017=AXIS2_PLACEMENT_3D ( 'NONE', #105136, #26162, #38461 ) ;
#17018=ADVANCED_FACE ( 'NONE', ( #10264 ), #53052, .F. ) ;
#17019=ORIENTED_EDGE ( 'NONE', *, *, #12573, .F. ) ;
#17020=DIRECTION ( 'NONE',  ( 0.7071067811865487940, -0.7071067811865463515, 0.000000000000000000 ) ) ;
#17021=VERTEX_POINT ( 'NONE', #64668 ) ;
#17022=EDGE_CURVE ( 'NONE', #31340, #26097, #65410, .T. ) ;
#17023=DIRECTION ( 'NONE',  ( 0.7071067811865486830, -0.7071067811865464625, -0.000000000000000000 ) ) ;
#17024=DIRECTION ( 'NONE',  ( -0.7071067811865487940, 0.7071067811865463515, 0.000000000000000000 ) ) ;
#17025=AXIS2_PLACEMENT_3D ( 'NONE', #116130, #18213, #105260 ) ;
#17027=EDGE_CURVE ( 'NONE', #28105, #137698, #74118, .T. ) ;
#17028=FACE_BOUND ( 'NONE', #2951, .T. ) ;
#17029=DIRECTION ( 'NONE',  ( 1.000000000000000000, 0.000000000000000000, 0.000000000000000000 ) ) ;
#17030=CARTESIAN_POINT ( 'NONE',  ( -26.99999999999980815, -9.033600742197648970, 5.000000000000000000 ) ) ;
#17032=EDGE_LOOP ( 'NONE', ( #60600, #104935, #128876 ) ) ;
#17033=VECTOR ( 'NONE', #26317, 1000.000000000000000 ) ;
#17034=EDGE_CURVE ( 'NONE', #745, #47403, #66113, .T. ) ;
#17037=VERTEX_POINT ( 'NONE', #84985 ) ;
#17038=VECTOR ( 'NONE', #138375, 999.9999999999998863 ) ;
#17039=ORIENTED_EDGE ( 'NONE', *, *, #38073, .T. ) ;
#17041=EDGE_LOOP ( 'NONE', ( #50439, #47263, #95344, #29623, #135931 ) ) ;
#17043=CARTESIAN_POINT ( 'NONE',  ( 45.18398860626900415, 28.73617430169818832, 5.000000000000000000 ) ) ;
#17044=LINE ( 'NONE', #61313, #7632 ) ;
#17045=VECTOR ( 'NONE', #125680, 1000.000000000000000 ) ;
#17047=ORIENTED_EDGE ( 'NONE', *, *, #58860, .T. ) ;
#17048=DIRECTION ( 'NONE',  ( -0.7071067811865486830, 0.7071067811865464625, 0.000000000000000000 ) ) ;
#17049=ADVANCED_FACE ( 'NONE', ( #19016 ), #100855, .F. ) ;
#17057=VERTEX_POINT ( 'NONE', #124748 ) ;
#17058=FACE_OUTER_BOUND ( 'NONE', #13517, .T. ) ;
#17059=CARTESIAN_POINT ( 'NONE',  ( -32.99999999999977263, -21.41253812416053037, 4.000000000000000000 ) ) ;
#17060=VECTOR ( 'NONE', #105784, 1000.000000000000000 ) ;
#17061=VERTEX_POINT ( 'NONE', #90719 ) ;
#17064=EDGE_LOOP ( 'NONE', ( #46098, #31323, #25421, #89404 ) ) ;
#17066=VERTEX_POINT ( 'NONE', #22547 ) ;
#17067=VECTOR ( 'NONE', #30796, 1000.000000000000000 ) ;
#17068=EDGE_CURVE ( 'NONE', #45188, #10027, #69, .T. ) ;
#17069=VECTOR ( 'NONE', #37029, 1000.000000000000000 ) ;
#17072=ORIENTED_EDGE ( 'NONE', *, *, #38798, .F. ) ;
#17073=DIRECTION ( 'NONE',  ( -0.000000000000000000, 0.000000000000000000, 1.000000000000000000 ) ) ;
#17074=ORIENTED_EDGE ( 'NONE', *, *, #38299, .F. ) ;
#17075=CARTESIAN_POINT ( 'NONE',  ( 11.99451991528749417, 28.92564299267946382, 4.000000000000000000 ) ) ;
#17076=CIRCLE ( 'NONE', #139735, 5.968999999999998529 ) ;
#17078=DIRECTION ( 'NONE',  ( -0.6830127018922180770, -0.6830127018922204085, -0.2588190451025213501 ) ) ;
#17079=ORIENTED_EDGE ( 'NONE', *, *, #99781, .F. ) ;
#17080=VERTEX_POINT ( 'NONE', #11668 ) ;
#17081=LINE ( 'NONE', #36672, #79363 ) ;
#17082=CARTESIAN_POINT ( 'NONE',  ( -3.469446951953614189E-15, -9.412538124160651165, 4.000000000000000000 ) ) ;
#17083=EDGE_LOOP ( 'NONE', ( #17310, #68930, #117046, #94123 ) ) ;
#17084=EDGE_CURVE ( 'NONE', #62679, #138950, #12408, .T. ) ;
#17085=FACE_OUTER_BOUND ( 'NONE', #109905, .T. ) ;
#17086=VERTEX_POINT ( 'NONE', #133498 ) ;
#17087=ORIENTED_EDGE ( 'NONE', *, *, #55588, .T. ) ;
#17088=ORIENTED_EDGE ( 'NONE', *, *, #12082, .F. ) ;
#17089=VERTEX_POINT ( 'NONE', #99398 ) ;
#17091=AXIS2_PLACEMENT_3D ( 'NONE', #62043, #93923, #72942 ) ;
#17092=LINE ( 'NONE', #40300, #81769 ) ;
#17095=EDGE_CURVE ( 'NONE', #41252, #127203, #122597, .T. ) ;
#17096=ORIENTED_EDGE ( 'NONE', *, *, #67932, .T. ) ;
#17097=FACE_OUTER_BOUND ( 'NONE', #19744, .T. ) ;
#17098=AXIS2_PLACEMENT_3D ( 'NONE', #81214, #111113, #137003 ) ;
#17099=ORIENTED_EDGE ( 'NONE', *, *, #115643, .F. ) ;
#17100=DIRECTION ( 'NONE',  ( -0.000000000000000000, 0.3543493200069153248, 0.9351131265310292928 ) ) ;
#17102=LINE ( 'NONE', #92494, #104128 ) ;
#17104=DIRECTION ( 'NONE',  ( -0.7071067811865486830, -0.7071067811865464625, -0.000000000000000000 ) ) ;
#17105=PLANE ( 'NONE',  #97605 ) ;
#17106=ORIENTED_EDGE ( 'NONE', *, *, #68943, .T. ) ;
#17107=ORIENTED_EDGE ( 'NONE', *, *, #80434, .T. ) ;
#17108=ORIENTED_EDGE ( 'NONE', *, *, #99160, .T. ) ;
#17109=CARTESIAN_POINT ( 'NONE',  ( 20.16170612452607358, -6.740707523384209310, 16.75550250614871928 ) ) ;
#17112=CARTESIAN_POINT ( 'NONE',  ( 11.70025512860841133, -27.71228299555198049, 4.000000000000000000 ) ) ;
#17117=CARTESIAN_POINT ( 'NONE',  ( 41.99451991528749062, 28.92564299267967343, 4.000000000000000000 ) ) ;
#17118=LINE ( 'NONE', #127294, #13101 ) ;
#17119=DIRECTION ( 'NONE',  ( -0.7071067811865487940, 0.7071067811865463515, -0.000000000000000000 ) ) ;
#17120=LINE ( 'NONE', #95386, #109023 ) ;
#17121=EDGE_LOOP ( 'NONE', ( #28099, #53632, #63589, #27610, #79779, #46093 ) ) ;
#17122=CARTESIAN_POINT ( 'NONE',  ( -27.48921356237309155, -27.52281430457074762, 5.000000000000000000 ) ) ;
#17123=VERTEX_POINT ( 'NONE', #1509 ) ;
#17125=DIRECTION ( 'NONE',  ( -0.3543493200069162685, -0.000000000000000000, -0.9351131265310288487 ) ) ;
#17126=LINE ( 'NONE', #49058, #18650 ) ;
#17127=ORIENTED_EDGE ( 'NONE', *, *, #58693, .F. ) ;
#17128=SPHERICAL_SURFACE ( 'NONE', #67980, 0.5000000000000000000 ) ;
#17129=CARTESIAN_POINT ( 'NONE',  ( -27.48921356237309155, -27.52281430457074762, 5.000000000000000000 ) ) ;
#17131=EDGE_LOOP ( 'NONE', ( #75288, #43806, #73065 ) ) ;
#17132=ORIENTED_EDGE ( 'NONE', *, *, #112990, .F. ) ;
#17133=DIRECTION ( 'NONE',  ( -0.6830127018922181881, 0.6830127018922202975, -0.2588190451025214056 ) ) ;
#17135=VECTOR ( 'NONE', #75202, 1000.000000000000000 ) ;
#17136=DIRECTION ( 'NONE',  ( 0.7071067811865487940, 0.7071067811865463515, -0.000000000000000000 ) ) ;
#17137=EDGE_CURVE ( 'NONE', #67449, #1511, #36326, .T. ) ;
#17141=VECTOR ( 'NONE', #39274, 1000.000000000000227 ) ;
#17142=FACE_OUTER_BOUND ( 'NONE', #21288, .T. ) ;
#17144=ADVANCED_FACE ( 'NONE', ( #34909 ), #100158, .T. ) ;
#17147=LINE ( 'NONE', #17827, #41487 ) ;
#17149=CARTESIAN_POINT ( 'NONE',  ( -15.68879807097514956, -1.757674993583058898, 4.000000000000000000 ) ) ;
#17150=PLANE ( 'NONE',  #16631 ) ;
#17151=ADVANCED_FACE ( 'NONE', ( #113140 ), #25419, .F. ) ;
#17152=VERTEX_POINT ( 'NONE', #24019 ) ;
#17153=CARTESIAN_POINT ( 'NONE',  ( -25.49999999999982236, -11.94781430457071103, 5.000000000000000000 ) ) ;
#17154=ADVANCED_FACE ( 'NONE', ( #44369 ), #34185, .F. ) ;
#17155=ORIENTED_EDGE ( 'NONE', *, *, #132793, .T. ) ;
#17159=DIRECTION ( 'NONE',  ( -0.000000000000000000, -1.000000000000000000, -0.000000000000000000 ) ) ;
#17160=DIRECTION ( 'NONE',  ( -1.000000000000000000, 0.000000000000000000, -0.000000000000000000 ) ) ;
#17161=VERTEX_POINT ( 'NONE', #46532 ) ;
#17162=CARTESIAN_POINT ( 'NONE',  ( -25.49999999999981171, 22.08746187583901843, 4.000000000000000000 ) ) ;
#17163=AXIS2_PLACEMENT_3D ( 'NONE', #54572, #118362, #140150 ) ;
#17164=ADVANCED_FACE ( 'NONE', ( #45098 ), #23271, .F. ) ;
#17166=VECTOR ( 'NONE', #118891, 999.9999999999998863 ) ;
#17167=PLANE ( 'NONE',  #143509 ) ;
#17168=DIRECTION ( 'NONE',  ( -0.7071067811865486830, -0.7071067811865464625, -0.000000000000000000 ) ) ;
#17169=ORIENTED_EDGE ( 'NONE', *, *, #26330, .F. ) ;
#17170=CARTESIAN_POINT ( 'NONE',  ( 51.18398860626899705, 28.73617430169823095, 5.000000000000000000 ) ) ;
#17171=CARTESIAN_POINT ( 'NONE',  ( -23.03315071937583980, 7.620612595215163765, 4.000000000000000000 ) ) ;
#17173=EDGE_CURVE ( 'NONE', #15103, #99152, #82004, .T. ) ;
#17174=CARTESIAN_POINT ( 'NONE',  ( -54.48921356237310221, -27.52281430457093236, 5.000000000000000000 ) ) ;
#17175=AXIS2_PLACEMENT_3D ( 'NONE', #90525, #136870, #135470 ) ;
#17176=VERTEX_POINT ( 'NONE', #115250 ) ;
#17177=EDGE_LOOP ( 'NONE', ( #124029, #69148, #22987, #53212 ) ) ;
#17181=FACE_OUTER_BOUND ( 'NONE', #107031, .T. ) ;
#17184=ORIENTED_EDGE ( 'NONE', *, *, #139362, .F. ) ;
#17185=LINE ( 'NONE', #74439, #32947 ) ;
#17186=LINE ( 'NONE', #49123, #83809 ) ;
#17188=ORIENTED_EDGE ( 'NONE', *, *, #24340, .T. ) ;
#17189=CARTESIAN_POINT ( 'NONE',  ( 25.49999999999981526, -11.94781430457070215, 5.000000000000000000 ) ) ;
#17190=EDGE_CURVE ( 'NONE', #129678, #50577, #115991, .T. ) ;
#17192=CIRCLE ( 'NONE', #91309, 5.968999999999998529 ) ;
#17194=EDGE_CURVE ( 'NONE', #75175, #123070, #82687, .T. ) ;
#17195=ORIENTED_EDGE ( 'NONE', *, *, #33873, .F. ) ;
#17197=CARTESIAN_POINT ( 'NONE',  ( 1.499999999999990896, 3.653845994658389884, -4.504631822206375702 ) ) ;
#17198=CARTESIAN_POINT ( 'NONE',  ( 1.171830600776463838, -14.24070752338414358, 4.000000000000000000 ) ) ;
#17199=LINE ( 'NONE', #26644, #102089 ) ;
#17201=ADVANCED_FACE ( 'NONE', ( #92105 ), #4321, .F. ) ;
#17202=LINE ( 'NONE', #38955, #21102 ) ;
#17204=ORIENTED_EDGE ( 'NONE', *, *, #128984, .F. ) ;
#17205=VERTEX_POINT ( 'NONE', #60977 ) ;
#17206=ORIENTED_EDGE ( 'NONE', *, *, #30383, .T. ) ;
#17207=ADVANCED_FACE ( 'NONE', ( #113871 ), #71825, .T. ) ;
#17208=VERTEX_POINT ( 'NONE', #126868 ) ;
#17209=AXIS2_PLACEMENT_3D ( 'NONE', #26326, #132446, #45427 ) ;
#17210=PLANE ( 'NONE',  #59395 ) ;
#17212=ORIENTED_EDGE ( 'NONE', *, *, #76926, .F. ) ;
#17215=CARTESIAN_POINT ( 'NONE',  ( 2.510786437626908008, -27.52281430457053446, 5.000000000000000000 ) ) ;
#17216=LINE ( 'NONE', #74476, #4441 ) ;
#17218=EDGE_LOOP ( 'NONE', ( #6845, #26789, #61714, #30068, #135587, #74553 ) ) ;
#17219=DIRECTION ( 'NONE',  ( -0.7071067811865486830, -0.7071067811865464625, 0.000000000000000000 ) ) ;
#17220=CARTESIAN_POINT ( 'NONE',  ( 31.49999999999978684, 0.05218569542916537407, 5.000000000000000000 ) ) ;
#17223=ORIENTED_EDGE ( 'NONE', *, *, #265, .T. ) ;
#17224=EDGE_CURVE ( 'NONE', #78506, #76045, #103678, .T. ) ;
#17226=ORIENTED_EDGE ( 'NONE', *, *, #76840, .T. ) ;
#17227=ORIENTED_EDGE ( 'NONE', *, *, #17842, .F. ) ;
#17229=VECTOR ( 'NONE', #77007, 1000.000000000000000 ) ;
#17230=ORIENTED_EDGE ( 'NONE', *, *, #29375, .T. ) ;
#17231=DIRECTION ( 'NONE',  ( -0.7071067811865487940, 0.7071067811865463515, 0.000000000000000000 ) ) ;
#17233=CARTESIAN_POINT ( 'NONE',  ( 5.999999999999970690, 5.587461875839184522, 4.000000000000000000 ) ) ;
#17235=DIRECTION ( 'NONE',  ( 0.7071067811865486830, -0.7071067811865464625, -0.000000000000000000 ) ) ;
#17236=VECTOR ( 'NONE', #58386, 1000.000000000000000 ) ;
#17237=CARTESIAN_POINT ( 'NONE',  ( -48.29974487139158867, -27.71228299555239971, 4.000000000000000000 ) ) ;
#17238=DIRECTION ( 'NONE',  ( -0.6830127018922180770, -0.6830127018922204085, -0.2588190451025213501 ) ) ;
#17239=DIRECTION ( 'NONE',  ( 0.7071067811865487940, -0.7071067811865463515, 0.000000000000000000 ) ) ;
#17240=ADVANCED_FACE ( 'NONE', ( #126184 ), #26859, .F. ) ;
#17241=LINE ( 'NONE', #48445, #90713 ) ;
#17242=LINE ( 'NONE', #61505, #70703 ) ;
#17243=EDGE_LOOP ( 'NONE', ( #36555, #2940, #78777 ) ) ;
#17244=ADVANCED_FACE ( 'NONE', ( #83398 ), #29010, .F. ) ;
#17245=PLANE ( 'NONE',  #50373 ) ;
#17246=VECTOR ( 'NONE', #89145, 999.9999999999998863 ) ;
#17247=DIRECTION ( 'NONE',  ( 0.7071067811865487940, -0.7071067811865463515, 0.000000000000000000 ) ) ;
#17248=ORIENTED_EDGE ( 'NONE', *, *, #63682, .F. ) ;
#17251=EDGE_LOOP ( 'NONE', ( #38518, #38764, #131382, #124818 ) ) ;
#17252=LINE ( 'NONE', #20087, #97659 ) ;
#17253=PLANE ( 'NONE',  #80241 ) ;
#17254=LINE ( 'NONE', #83979, #120359 ) ;
#17256=CARTESIAN_POINT ( 'NONE',  ( 17.35681257248251086, -20.24070752338407431, 21.22881796311217073 ) ) ;
#17257=VERTEX_POINT ( 'NONE', #5791 ) ;
#17259=ORIENTED_EDGE ( 'NONE', *, *, #100147, .F. ) ;
#17262=VECTOR ( 'NONE', #98922, 1000.000000000000000 ) ;
#17263=CARTESIAN_POINT ( 'NONE',  ( 15.18398860626900237, 28.73617430169797871, 5.000000000000000000 ) ) ;
#17264=VECTOR ( 'NONE', #134745, 1000.000000000000000 ) ;
#17266=VERTEX_POINT ( 'NONE', #94954 ) ;
#17270=CARTESIAN_POINT ( 'NONE',  ( 18.29974487139159223, -27.71228299555219010, 4.000000000000000000 ) ) ;
#17271=PLANE ( 'NONE',  #107502 ) ;
#17273=CARTESIAN_POINT ( 'NONE',  ( 12.18398860626900060, 28.73617430169795739, 5.000000000000000000 ) ) ;
#17275=VECTOR ( 'NONE', #48247, 1000.000000000000227 ) ;
#17278=CARTESIAN_POINT ( 'NONE',  ( 32.99451991528749062, 28.92564299267960948, 4.000000000000000000 ) ) ;
#17280=CARTESIAN_POINT ( 'NONE',  ( -12.64318742751729907, -20.24070752338407075, 21.22881796311209612 ) ) ;
#17281=CARTESIAN_POINT ( 'NONE',  ( 0.000000000000000000, 12.25461709320620507, -10.07315571508697261 ) ) ;
#17282=ORIENTED_EDGE ( 'NONE', *, *, #124140, .F. ) ;
#17283=DIRECTION ( 'NONE',  ( 0.6830127018922181881, 0.6830127018922202975, -0.2588190451025214056 ) ) ;
#17284=DIRECTION ( 'NONE',  ( 0.7071067811865486830, -0.7071067811865464625, -0.000000000000000000 ) ) ;
#17286=LINE ( 'NONE', #138362, #102418 ) ;
#17288=ORIENTED_EDGE ( 'NONE', *, *, #84605, .F. ) ;
#17289=PLANE ( 'NONE',  #60523 ) ;
#17291=ORIENTED_EDGE ( 'NONE', *, *, #26796, .T. ) ;
#17292=CARTESIAN_POINT ( 'NONE',  ( 35.99451991528749772, 28.92564299267963079, 4.000000000000000000 ) ) ;
#17294=EDGE_CURVE ( 'NONE', #139679, #92329, #14563, .T. ) ;
#17295=CARTESIAN_POINT ( 'NONE',  ( 20.29289321881332242, -15.74070752338412049, 5.000000000000000000 ) ) ;
#17296=DIRECTION ( 'NONE',  ( 0.7071067811865487940, 0.7071067811865463515, 0.000000000000000000 ) ) ;
#17297=ADVANCED_FACE ( 'NONE', ( #61662 ), #27555, .F. ) ;
#17298=EDGE_CURVE ( 'NONE', #140272, #29472, #139222, .T. ) ;
#17299=DIRECTION ( 'NONE',  ( -0.7071067811865486830, -0.7071067811865464625, 0.000000000000000000 ) ) ;
#17300=PLANE ( 'NONE',  #61075 ) ;
#17301=EDGE_CURVE ( 'NONE', #86059, #34296, #92827, .T. ) ;
#17302=CARTESIAN_POINT ( 'NONE',  ( 39.48921356237310221, -27.52281430457082934, 5.000000000000000000 ) ) ;
#17305=LINE ( 'NONE', #26057, #66755 ) ;
#17306=LINE ( 'NONE', #17985, #112679 ) ;
#17307=ADVANCED_FACE ( 'NONE', ( #39918 ), #128338, .F. ) ;
#17308=VERTEX_POINT ( 'NONE', #47941 ) ;
#17309=VECTOR ( 'NONE', #47081, 1000.000000000000000 ) ;
#17310=ORIENTED_EDGE ( 'NONE', *, *, #8258, .T. ) ;
#17312=LINE ( 'NONE', #118761, #111501 ) ;
#17313=ORIENTED_EDGE ( 'NONE', *, *, #1762, .T. ) ;
#17314=EDGE_CURVE ( 'NONE', #43657, #70215, #37024, .T. ) ;
#17315=FACE_OUTER_BOUND ( 'NONE', #92051, .T. ) ;
#17317=DIRECTION ( 'NONE',  ( 0.6830127018922181881, 0.6830127018922202975, -0.2588190451025214056 ) ) ;
#17318=ORIENTED_EDGE ( 'NONE', *, *, #137828, .F. ) ;
#17319=CARTESIAN_POINT ( 'NONE',  ( 8.293207492759204769, 20.25929247661551358, 20.83292124670812839 ) ) ;
#17320=CARTESIAN_POINT ( 'NONE',  ( -21.33010218547252279, 17.25929247661553845, 19.83885114516075987 ) ) ;
#17321=EDGE_CURVE ( 'NONE', #123762, #13717, #53629, .T. ) ;
#17322=CARTESIAN_POINT ( 'NONE',  ( 34.49999999999975842, 15.43112307739203004, 4.000000000000000000 ) ) ;
#17323=DIRECTION ( 'NONE',  ( 0.7071067811865486830, -0.7071067811865464625, -0.000000000000000000 ) ) ;
#17324=EDGE_CURVE ( 'NONE', #28047, #108474, #62367, .T. ) ;
#17325=LINE ( 'NONE', #71026, #74854 ) ;
#17326=FACE_OUTER_BOUND ( 'NONE', #125456, .T. ) ;
#17328=CARTESIAN_POINT ( 'NONE',  ( -2.510786437626908008, -27.52281430457053446, 5.000000000000000000 ) ) ;
#17329=CARTESIAN_POINT ( 'NONE',  ( 2.483345613589531542, 22.22500000000000142, 4.500000000000000888 ) ) ;
#17330=DIRECTION ( 'NONE',  ( 0.7071067811865486830, -0.7071067811865464625, -0.000000000000000000 ) ) ;
#17332=EDGE_CURVE ( 'NONE', #1839, #55182, #31167, .T. ) ;
#17333=DIRECTION ( 'NONE',  ( -0.000000000000000000, -0.3543493200069152693, 0.9351131265310292928 ) ) ;
#17334=VECTOR ( 'NONE', #26612, 1000.000000000000000 ) ;
#17335=VERTEX_POINT ( 'NONE', #8627 ) ;
#17336=VERTEX_POINT ( 'NONE', #131898 ) ;
#17338=ORIENTED_EDGE ( 'NONE', *, *, #55299, .F. ) ;
#17340=DIRECTION ( 'NONE',  ( 0.3543493200069162685, -0.000000000000000000, -0.9351131265310288487 ) ) ;
#17341=CARTESIAN_POINT ( 'NONE',  ( -17.70025512860841488, -27.71228299555193786, 4.000000000000000000 ) ) ;
#17342=EDGE_LOOP ( 'NONE', ( #29275, #2980, #20814, #27365 ) ) ;
#17344=DIRECTION ( 'NONE',  ( 0.7071067811865487940, 0.7071067811865463515, 0.000000000000000000 ) ) ;
#17346=VECTOR ( 'NONE', #135691, 1000.000000000000000 ) ;
#17347=ORIENTED_EDGE ( 'NONE', *, *, #84683, .F. ) ;
#17348=FACE_OUTER_BOUND ( 'NONE', #48317, .T. ) ;
#17349=ORIENTED_EDGE ( 'NONE', *, *, #23989, .T. ) ;
#17350=CARTESIAN_POINT ( 'NONE',  ( 22.04515773336653695, -21.74070752338405654, 21.72585301388589585 ) ) ;
#17351=EDGE_CURVE ( 'NONE', #119366, #83686, #119549, .T. ) ;
#17352=DIRECTION ( 'NONE',  ( 0.7071067811865486830, -0.7071067811865464625, -0.000000000000000000 ) ) ;
#17353=FACE_OUTER_BOUND ( 'NONE', #142231, .T. ) ;
#17354=DIRECTION ( 'NONE',  ( -0.6830127018922180770, -0.6830127018922204085, -0.2588190451025213501 ) ) ;
#17355=ORIENTED_EDGE ( 'NONE', *, *, #25732, .T. ) ;
#17356=ORIENTED_EDGE ( 'NONE', *, *, #51219, .F. ) ;
#17357=EDGE_LOOP ( 'NONE', ( #72681, #129649, #25397, #91221 ) ) ;
#17358=DIRECTION ( 'NONE',  ( -0.3543493200069162685, -0.000000000000000000, -0.9351131265310288487 ) ) ;
#17359=DIRECTION ( 'NONE',  ( 0.7071067811865487940, 0.7071067811865463515, 0.000000000000000000 ) ) ;
#17361=DIRECTION ( 'NONE',  ( 0.7071067811865487940, 0.7071067811865463515, -0.000000000000000000 ) ) ;
#17362=VECTOR ( 'NONE', #43199, 1000.000000000000000 ) ;
#17363=FILL_AREA_STYLE_COLOUR ( '', #23755 ) ;
#17364=AXIS2_PLACEMENT_3D ( 'NONE', #93752, #6688, #72768 ) ;
#17366=VERTEX_POINT ( 'NONE', #109419 ) ;
#17368=EDGE_LOOP ( 'NONE', ( #45009, #388, #78434, #128650 ) ) ;
#17369=CARTESIAN_POINT ( 'NONE',  ( 50.99451991528749062, 28.92564299267973738, 4.000000000000000000 ) ) ;
#17370=EDGE_CURVE ( 'NONE', #36339, #88739, #73244, .T. ) ;
#17371=ORIENTED_EDGE ( 'NONE', *, *, #98286, .F. ) ;
#17372=EDGE_LOOP ( 'NONE', ( #63428, #64168, #113003, #82662 ) ) ;
#17375=DIRECTION ( 'NONE',  ( 0.7071067811865487940, -0.7071067811865463515, 0.000000000000000000 ) ) ;
#17376=ORIENTED_EDGE ( 'NONE', *, *, #48645, .T. ) ;
#17377=CARTESIAN_POINT ( 'NONE',  ( -2.207106781186530586, 6.759292476615651246, 5.000000000000000000 ) ) ;
#17378=EDGE_CURVE ( 'NONE', #55777, #137620, #52870, .T. ) ;
#17380=DIRECTION ( 'NONE',  ( 1.000000000000000000, 0.000000000000000000, 0.000000000000000000 ) ) ;
#17381=DIRECTION ( 'NONE',  ( 0.3543493200069162685, -0.000000000000000000, -0.9351131265310288487 ) ) ;
#17382=ORIENTED_EDGE ( 'NONE', *, *, #104405, .T. ) ;
#17383=DIRECTION ( 'NONE',  ( 0.7071067811865487940, 0.7071067811865463515, 0.000000000000000000 ) ) ;
#17384=FACE_BOUND ( 'NONE', #6648, .T. ) ;
#17385=EDGE_LOOP ( 'NONE', ( #85166, #3643, #66790, #43738 ) ) ;
#17387=DIRECTION ( 'NONE',  ( 0.3543493200069162685, -0.000000000000000000, -0.9351131265310288487 ) ) ;
#17389=EDGE_LOOP ( 'NONE', ( #85050, #128031, #82158, #142943 ) ) ;
#17390=DIRECTION ( 'NONE',  ( -0.000000000000000000, 0.3543493200069153248, 0.9351131265310292928 ) ) ;
#17393=ORIENTED_EDGE ( 'NONE', *, *, #88418, .F. ) ;
#17395=EDGE_LOOP ( 'NONE', ( #32486, #41347, #130300, #99301 ) ) ;
#17396=CARTESIAN_POINT ( 'NONE',  ( 2.292893218813435219, 14.25929247661557753, 5.000000000000000000 ) ) ;
#17398=DIRECTION ( 'NONE',  ( -0.000000000000000000, -0.3543493200069152693, 0.9351131265310292928 ) ) ;
#17400=CARTESIAN_POINT ( 'NONE',  ( 5.538396446294259867, -9.740707523384180888, 17.74957260769611977 ) ) ;
#17401=LINE ( 'NONE', #96360, #12514 ) ;
#17402=CARTESIAN_POINT ( 'NONE',  ( -11.99999999999991296, 4.384688058510558761, -7.090945410444713382 ) ) ;
#17403=LINE ( 'NONE', #126865, #143221 ) ;
#17404=EDGE_CURVE ( 'NONE', #119665, #68775, #141330, .T. ) ;
#17406=EDGE_CURVE ( 'NONE', #69796, #35696, #96365, .T. ) ;
#17407=EDGE_LOOP ( 'NONE', ( #91509, #91597, #87698, #34911 ) ) ;
#17408=ORIENTED_EDGE ( 'NONE', *, *, #59702, .F. ) ;
#17409=ORIENTED_EDGE ( 'NONE', *, *, #112715, .F. ) ;
#17411=DIRECTION ( 'NONE',  ( -0.3543493200069162685, -0.000000000000000000, -0.9351131265310288487 ) ) ;
#17412=ORIENTED_EDGE ( 'NONE', *, *, #31217, .F. ) ;
#17413=( BOUNDED_CURVE ( )  B_SPLINE_CURVE ( 3, ( #36351, #46557, #79174, #13131 ),
 .UNSPECIFIED., .F., .F. ) 
 B_SPLINE_CURVE_WITH_KNOTS ( ( 4, 4 ),
 ( 2.001653308786169649, 3.503810798801450854 ),
 .UNSPECIFIED. ) 
 CURVE ( )  GEOMETRIC_REPRESENTATION_ITEM ( )  RATIONAL_B_SPLINE_CURVE ( ( 1.000000000000000000, 0.8206354192515240564, 0.8206354192515240564, 1.000000000000000000 ) ) 
 REPRESENTATION_ITEM ( '' )  );
#17415=CARTESIAN_POINT ( 'NONE',  ( -27.18398860626900060, 28.73617430169806042, 5.000000000000000000 ) ) ;
#17416=CARTESIAN_POINT ( 'NONE',  ( 11.51078643762690490, -27.52281430457047406, 5.000000000000000000 ) ) ;
#17417=EDGE_CURVE ( 'NONE', #4524, #75885, #95681, .T. ) ;
#17420=ORIENTED_EDGE ( 'NONE', *, *, #45777, .T. ) ;
#17421=DIRECTION ( 'NONE',  ( 1.000000000000000000, 0.000000000000000000, 0.000000000000000000 ) ) ;
#17422=ORIENTED_EDGE ( 'NONE', *, *, #105538, .F. ) ;
#17423=CARTESIAN_POINT ( 'NONE',  ( 5.207106781186515931, 6.759292476615653023, 5.000000000000000000 ) ) ;
#17424=VECTOR ( 'NONE', #103271, 1000.000000000000000 ) ;
#17425=PLANE ( 'NONE',  #91386 ) ;
#17427=ORIENTED_EDGE ( 'NONE', *, *, #41221, .T. ) ;
#17430=VECTOR ( 'NONE', #83724, 1000.000000000000000 ) ;
#17433=ORIENTED_EDGE ( 'NONE', *, *, #21110, .F. ) ;
#17434=ORIENTED_EDGE ( 'NONE', *, *, #139883, .F. ) ;
#17435=LINE ( 'NONE', #61692, #12593 ) ;
#17436=VERTEX_POINT ( 'NONE', #98540 ) ;
#17437=CARTESIAN_POINT ( 'NONE',  ( -2.282422613574296655, -21.73023691814492153, 5.000000000000000888 ) ) ;
#17438=LINE ( 'NONE', #82034, #29165 ) ;
#17439=FACE_OUTER_BOUND ( 'NONE', #60965, .T. ) ;
#17440=DIRECTION ( 'NONE',  ( -0.7071067811865486830, -0.7071067811865464625, 0.000000000000000000 ) ) ;
#17442=ORIENTED_EDGE ( 'NONE', *, *, #86746, .T. ) ;
#17443=LINE ( 'NONE', #126221, #8889 ) ;
#17445=CARTESIAN_POINT ( 'NONE',  ( 34.92499999999998295, -19.48753812416032716, 4.000000000000000000 ) ) ;
#17446=LINE ( 'NONE', #5111, #19054 ) ;
#17447=VERTEX_POINT ( 'NONE', #142078 ) ;
#17448=DIRECTION ( 'NONE',  ( 0.6830127018922181881, 0.6830127018922202975, -0.2588190451025214056 ) ) ;
#17450=ORIENTED_EDGE ( 'NONE', *, *, #39835, .F. ) ;
#17452=ORIENTED_EDGE ( 'NONE', *, *, #18592, .F. ) ;
#17453=VERTEX_POINT ( 'NONE', #140607 ) ;
#17458=EDGE_CURVE ( 'NONE', #72549, #14195, #29698, .T. ) ;
#17460=VECTOR ( 'NONE', #66042, 1000.000000000000227 ) ;
#17461=ADVANCED_FACE ( 'NONE', ( #19551 ), #129023, .F. ) ;
#17462=FACE_OUTER_BOUND ( 'NONE', #23496, .T. ) ;
#17465=EDGE_CURVE ( 'NONE', #108894, #31809, #20970, .T. ) ;
#17466=CARTESIAN_POINT ( 'NONE',  ( 0.000000000000000000, 0.000000000000000000, 5.000000000000000000 ) ) ;
#17468=LINE ( 'NONE', #61039, #141583 ) ;
#17469=DIRECTION ( 'NONE',  ( -0.7071067811865486830, 0.7071067811865464625, 0.000000000000000000 ) ) ;
#17471=PLANE ( 'NONE',  #78445 ) ;
#17472=VECTOR ( 'NONE', #43883, 1000.000000000000000 ) ;
#17473=FACE_OUTER_BOUND ( 'NONE', #134269, .T. ) ;
#17474=LINE ( 'NONE', #61729, #140317 ) ;
#17476=VERTEX_POINT ( 'NONE', #18085 ) ;
#17477=ADVANCED_FACE ( 'NONE', ( #107268 ), #31865, .F. ) ;
#17478=ORIENTED_EDGE ( 'NONE', *, *, #128627, .T. ) ;
#17479=VERTEX_POINT ( 'NONE', #85501 ) ;
#17481=ORIENTED_EDGE ( 'NONE', *, *, #69953, .T. ) ;
#17482=ORIENTED_EDGE ( 'NONE', *, *, #20259, .F. ) ;
#17483=ORIENTED_EDGE ( 'NONE', *, *, #106004, .T. ) ;
#17484=DIRECTION ( 'NONE',  ( 1.000000000000000000, 0.000000000000000000, 0.000000000000000000 ) ) ;
#17485=VERTEX_POINT ( 'NONE', #23087 ) ;
#17487=FACE_OUTER_BOUND ( 'NONE', #50689, .T. ) ;
#17488=EDGE_CURVE ( 'NONE', #38637, #72848, #134782, .T. ) ;
#17489=CARTESIAN_POINT ( 'NONE',  ( -36.18398860626899705, 28.73617430169812437, 5.000000000000000000 ) ) ;
#17492=ORIENTED_EDGE ( 'NONE', *, *, #128472, .F. ) ;
#17493=ADVANCED_FACE ( 'NONE', ( #122424 ), #12943, .T. ) ;
#17495=CARTESIAN_POINT ( 'NONE',  ( 3.489213562373097322, -27.52281430457057709, 5.000000000000000000 ) ) ;
#17496=DIRECTION ( 'NONE',  ( 1.000000000000000000, 0.000000000000000000, 0.000000000000000000 ) ) ;
#17498=DIRECTION ( 'NONE',  ( -0.6830127018922181881, 0.6830127018922202975, -0.2588190451025214056 ) ) ;
#17501=EDGE_CURVE ( 'NONE', #81904, #63910, #33337, .T. ) ;
#17502=CARTESIAN_POINT ( 'NONE',  ( 45.48921356237309510, -27.52281430457087197, 5.000000000000000000 ) ) ;
#17503=CARTESIAN_POINT ( 'NONE',  ( 25.49999999999982947, 10.46639925780215208, 5.000000000000000000 ) ) ;
#17505=EDGE_LOOP ( 'NONE', ( #267, #15186, #114321, #87575 ) ) ;
#17508=PLANE ( 'NONE',  #140924 ) ;
#17509=CARTESIAN_POINT ( 'NONE',  ( 34.42499999999998295, 0.000000000000000000, 4.500000000000000888 ) ) ;
#17510=ADVANCED_FACE ( 'NONE', ( #643 ), #11494, .F. ) ;
#17511=CARTESIAN_POINT ( 'NONE',  ( 18.70710678118641113, -6.740707523384205757, 5.000000000000000000 ) ) ;
#17512=DIRECTION ( 'NONE',  ( -0.000000000000000000, -0.000000000000000000, 1.000000000000000000 ) ) ;
#17515=CARTESIAN_POINT ( 'NONE',  ( 35.99451991528749772, 28.92564299267963079, 4.000000000000000000 ) ) ;
#17516=ORIENTED_EDGE ( 'NONE', *, *, #100401, .F. ) ;
#17517=EDGE_CURVE ( 'NONE', #114247, #75689, #34730, .T. ) ;
#17519=CARTESIAN_POINT ( 'NONE',  ( 4.499999999999966249, -19.53360074219753884, 5.000000000000000000 ) ) ;
#17520=CARTESIAN_POINT ( 'NONE',  ( -11.70025512860841133, -27.71228299555198049, 4.000000000000000000 ) ) ;
#17521=FACE_OUTER_BOUND ( 'NONE', #21105, .T. ) ;
#17522=ORIENTED_EDGE ( 'NONE', *, *, #82608, .T. ) ;
#17524=EDGE_LOOP ( 'NONE', ( #93835, #26509, #77809, #133429 ) ) ;
#17525=PLANE ( 'NONE',  #95647 ) ;
#17526=CARTESIAN_POINT ( 'NONE',  ( -18.48921356237309510, -27.52281430457068367, 5.000000000000000000 ) ) ;
#17527=DIRECTION ( 'NONE',  ( -0.000000000000000000, -0.000000000000000000, 1.000000000000000000 ) ) ;
#17528=ADVANCED_FACE ( 'NONE', ( #57219 ), #101396, .F. ) ;
#17529=EDGE_CURVE ( 'NONE', #80972, #133165, #123176, .T. ) ;
#17530=LINE ( 'NONE', #52303, #34521 ) ;
#17531=EDGE_CURVE ( 'NONE', #50205, #75083, #112295, .T. ) ;
#17532=VECTOR ( 'NONE', #107050, 999.9999999999998863 ) ;
#17536=CARTESIAN_POINT ( 'NONE',  ( -34.49999999999975131, 13.56627193232212392, -10.57019076586076700 ) ) ;
#17537=ORIENTED_EDGE ( 'NONE', *, *, #2032, .F. ) ;
#17538=ORIENTED_EDGE ( 'NONE', *, *, #126161, .F. ) ;
#17541=DIRECTION ( 'NONE',  ( 0.6830127018922180770, -0.6830127018922204085, -0.2588190451025214056 ) ) ;
#17543=CARTESIAN_POINT ( 'NONE',  ( 17.72082203615853047, 8.995094813919580545, 4.338987337627234098 ) ) ;
#17544=FACE_OUTER_BOUND ( 'NONE', #97678, .T. ) ;
#17545=FACE_BOUND ( 'NONE', #67227, .T. ) ;
#17546=LINE ( 'NONE', #94399, #103505 ) ;
#17548=FACE_OUTER_BOUND ( 'NONE', #35933, .T. ) ;
#17550=DIRECTION ( 'NONE',  ( 0.7071067811865487940, 0.7071067811865463515, 0.000000000000000000 ) ) ;
#17551=ORIENTED_EDGE ( 'NONE', *, *, #87257, .T. ) ;
#17552=ORIENTED_EDGE ( 'NONE', *, *, #60039, .T. ) ;
#17553=CARTESIAN_POINT ( 'NONE',  ( -29.99999999999979039, 11.96639925780214320, 5.000000000000000000 ) ) ;
#17555=ORIENTED_EDGE ( 'NONE', *, *, #42680, .F. ) ;
#17558=ORIENTED_EDGE ( 'NONE', *, *, #70265, .F. ) ;
#17559=AXIS2_PLACEMENT_3D ( 'NONE', #27596, #59556, #103712 ) ;
#17560=DIRECTION ( 'NONE',  ( 0.6830127018922181881, 0.6830127018922202975, -0.2588190451025214056 ) ) ;
#17561=VECTOR ( 'NONE', #77624, 1000.000000000000000 ) ;
#17562=CARTESIAN_POINT ( 'NONE',  ( 63.18398860626900415, 28.73617430169831621, 5.000000000000000000 ) ) ;
#17563=ORIENTED_EDGE ( 'NONE', *, *, #56667, .F. ) ;
#17564=PLANE ( 'NONE',  #39868 ) ;
#17566=PLANE ( 'NONE',  #29322 ) ;
#17567=CARTESIAN_POINT ( 'NONE',  ( 14.85700540165866634, 7.427722529079420433, 4.951096321256156507 ) ) ;
#17568=CARTESIAN_POINT ( 'NONE',  ( 12.48921356237309155, -27.52281430457064104, 5.000000000000000000 ) ) ;
#17569=FACE_OUTER_BOUND ( 'NONE', #72878, .T. ) ;
#17570=CARTESIAN_POINT ( 'NONE',  ( -11.81601139373100651, 28.73617430169779041, 5.000000000000000000 ) ) ;
#17571=ORIENTED_EDGE ( 'NONE', *, *, #48167, .T. ) ;
#17572=ORIENTED_EDGE ( 'NONE', *, *, #96871, .T. ) ;
#17573=DIRECTION ( 'NONE',  ( -0.7071067811865486830, -0.7071067811865464625, 0.000000000000000000 ) ) ;
#17575=ORIENTED_EDGE ( 'NONE', *, *, #63992, .F. ) ;
#17576=EDGE_LOOP ( 'NONE', ( #8261, #73218, #33340, #26233 ) ) ;
#17578=CARTESIAN_POINT ( 'NONE',  ( 18.48921356237309510, -27.52281430457068367, 5.000000000000000000 ) ) ;
#17579=EDGE_CURVE ( 'NONE', #114619, #18858, #66645, .T. ) ;
#17580=EDGE_CURVE ( 'NONE', #14634, #123707, #44936, .T. ) ;
#17581=CARTESIAN_POINT ( 'NONE',  ( -22.49999999999984368, 12.43112307739206024, 4.000000000000000000 ) ) ;
#17582=ORIENTED_EDGE ( 'NONE', *, *, #71832, .F. ) ;
#17583=CARTESIAN_POINT ( 'NONE',  ( 32.99999999999977973, 17.96639925780207747, 5.000000000000000000 ) ) ;
#17585=LINE ( 'NONE', #137975, #142134 ) ;
#17586=ORIENTED_EDGE ( 'NONE', *, *, #112507, .T. ) ;
#17588=ADVANCED_FACE ( 'NONE', ( #21701 ), #110114, .T. ) ;
#17589=CARTESIAN_POINT ( 'NONE',  ( -44.99451991528749772, 28.92564299267969474, 4.000000000000000000 ) ) ;
#17591=DIRECTION ( 'NONE',  ( 0.6830127018922180770, -0.6830127018922204085, -0.2588190451025213501 ) ) ;
#17592=EDGE_LOOP ( 'NONE', ( #108958, #127486, #13314, #26622 ) ) ;
#17594=PLANE ( 'NONE',  #3035 ) ;
#17595=ORIENTED_EDGE ( 'NONE', *, *, #116380, .T. ) ;
#17596=CARTESIAN_POINT ( 'NONE',  ( 0.000000000000000000, 0.000000000000000000, 5.000000000000000000 ) ) ;
#17599=EDGE_CURVE ( 'NONE', #28471, #116082, #55059, .T. ) ;
#17600=EDGE_LOOP ( 'NONE', ( #92171, #33463, #48996, #124004 ) ) ;
#17601=DIRECTION ( 'NONE',  ( -0.7071067811865486830, 0.7071067811865464625, 0.000000000000000000 ) ) ;
#17603=DIRECTION ( 'NONE',  ( 0.7071067811865486830, -0.7071067811865464625, -0.000000000000000000 ) ) ;
#17604=ORIENTED_EDGE ( 'NONE', *, *, #12866, .T. ) ;
#17605=EDGE_CURVE ( 'NONE', #49860, #64348, #34024, .T. ) ;
#17607=LINE ( 'NONE', #140144, #123470 ) ;
#17608=CARTESIAN_POINT ( 'NONE',  ( 6.836528711265448699, 15.75929247661555976, 9.299976744542933105 ) ) ;
#17609=CARTESIAN_POINT ( 'NONE',  ( 1.301042606982605321E-15, -21.41253812416053748, 4.000000000000000000 ) ) ;
#17610=CARTESIAN_POINT ( 'NONE',  ( 21.48921356237309155, -27.52281430457070499, 5.000000000000000000 ) ) ;
#17611=ORIENTED_EDGE ( 'NONE', *, *, #16644, .F. ) ;
#17612=EDGE_LOOP ( 'NONE', ( #7610, #45907, #52844, #70920 ) ) ;
#17613=FACE_OUTER_BOUND ( 'NONE', #14616, .T. ) ;
#17616=VECTOR ( 'NONE', #75024, 999.9999999999998863 ) ;
#17618=CARTESIAN_POINT ( 'NONE',  ( 24.00548008471250938, 28.92564299267921513, 4.000000000000000000 ) ) ;
#17619=DIRECTION ( 'NONE',  ( 0.7071067811865487940, 0.7071067811865463515, 0.000000000000000000 ) ) ;
#17620=AXIS2_PLACEMENT_3D ( 'NONE', #20915, #97021, #41991 ) ;
#17621=ORIENTED_EDGE ( 'NONE', *, *, #52558, .F. ) ;
#17623=FACE_OUTER_BOUND ( 'NONE', #58483, .T. ) ;
#17624=CARTESIAN_POINT ( 'NONE',  ( -11.67183060077638856, 5.259292476615662792, 4.000000000000000000 ) ) ;
#17625=DIRECTION ( 'NONE',  ( 0.7071067811865486830, -0.7071067811865464625, -0.000000000000000000 ) ) ;
#17626=DIRECTION ( 'NONE',  ( -0.000000000000000000, 0.000000000000000000, 1.000000000000000000 ) ) ;
#17628=LINE ( 'NONE', #139476, #60352 ) ;
#17629=EDGE_CURVE ( 'NONE', #127668, #903, #56493, .T. ) ;
#17630=EDGE_CURVE ( 'NONE', #131124, #140410, #23815, .T. ) ;
#17631=ORIENTED_EDGE ( 'NONE', *, *, #38250, .T. ) ;
#17633=ORIENTED_EDGE ( 'NONE', *, *, #115124, .T. ) ;
#17635=ORIENTED_EDGE ( 'NONE', *, *, #140237, .F. ) ;
#17636=CARTESIAN_POINT ( 'NONE',  ( -34.49999999999975131, 4.087461875839202285, 4.000000000000000000 ) ) ;
#17637=EDGE_CURVE ( 'NONE', #24661, #24394, #113662, .T. ) ;
#17638=CARTESIAN_POINT ( 'NONE',  ( -30.87485380690746695, -14.24070752338413826, 9.401115078912727796 ) ) ;
#17639=DIRECTION ( 'NONE',  ( -0.7071067811865486830, -0.7071067811865464625, 0.000000000000000000 ) ) ;
#17640=VECTOR ( 'NONE', #94709, 1000.000000000000000 ) ;
#17643=LINE ( 'NONE', #72095, #77798 ) ;
#17644=ORIENTED_EDGE ( 'NONE', *, *, #22169, .F. ) ;
#17645=EDGE_CURVE ( 'NONE', #26178, #82150, #68081, .T. ) ;
#17646=DIRECTION ( 'NONE',  ( -0.7071067811865486830, 0.7071067811865464625, 0.000000000000000000 ) ) ;
#17647=CARTESIAN_POINT ( 'NONE',  ( 54.18398860626899705, 28.73617430169825226, 5.000000000000000000 ) ) ;
#17648=CARTESIAN_POINT ( 'NONE',  ( 13.69176145124043131, 22.22500000000000142, -13.42270830385341363 ) ) ;
#17649=DIRECTION ( 'NONE',  ( 0.7071067811865486830, -0.7071067811865464625, -0.000000000000000000 ) ) ;
#17653=AXIS2_PLACEMENT_3D ( 'NONE', #68915, #110929, #68223 ) ;
#17654=CARTESIAN_POINT ( 'NONE',  ( -11.99999999999990941, 19.55218569542897100, 5.000000000000000000 ) ) ;
#17655=EDGE_LOOP ( 'NONE', ( #21265, #100236, #2172, #90403 ) ) ;
#17656=ORIENTED_EDGE ( 'NONE', *, *, #106500, .F. ) ;
#17658=EDGE_CURVE ( 'NONE', #88912, #29169, #33984, .T. ) ;
#17659=CARTESIAN_POINT ( 'NONE',  ( -9.316579611327837185, -6.740707523384216415, 11.88629033278126279 ) ) ;
#17660=DIRECTION ( 'NONE',  ( 0.7071067811865487940, 0.7071067811865463515, 0.000000000000000000 ) ) ;
#17663=ORIENTED_EDGE ( 'NONE', *, *, #7341, .T. ) ;
#17664=ADVANCED_FACE ( 'NONE', ( #101364 ), #3455, .F. ) ;
#17665=FACE_OUTER_BOUND ( 'NONE', #14766, .T. ) ;
#17666=CARTESIAN_POINT ( 'NONE',  ( 15.48921356237309510, -27.52281430457066236, 5.000000000000000000 ) ) ;
#17668=ORIENTED_EDGE ( 'NONE', *, *, #796, .F. ) ;
#17669=CARTESIAN_POINT ( 'NONE',  ( -15.29974487139158867, -27.71228299555216879, 4.000000000000000000 ) ) ;
#17670=VERTEX_POINT ( 'NONE', #91911 ) ;
#17671=ORIENTED_EDGE ( 'NONE', *, *, #116508, .T. ) ;
#17672=PLANE ( 'NONE',  #47030 ) ;
#17673=CARTESIAN_POINT ( 'NONE',  ( 7.499999999999940492, -1.912538124160725106, 4.000000000000000000 ) ) ;
#17674=CARTESIAN_POINT ( 'NONE',  ( -11.81601139373100651, 28.73617430169779041, 5.000000000000000000 ) ) ;
#17675=CARTESIAN_POINT ( 'NONE',  ( 27.48921356237309155, -27.52281430457074762, 5.000000000000000000 ) ) ;
#17676=CARTESIAN_POINT ( 'NONE',  ( -15.48921356237309510, -27.52281430457066236, 5.000000000000000000 ) ) ;
#17678=ORIENTED_EDGE ( 'NONE', *, *, #71755, .F. ) ;
#17679=LINE ( 'NONE', #116304, #129442 ) ;
#17680=LINE ( 'NONE', #128614, #3766 ) ;
#17681=LINE ( 'NONE', #82278, #26313 ) ;
#17682=EDGE_CURVE ( 'NONE', #9454, #66309, #11469, .T. ) ;
#17683=LINE ( 'NONE', #6785, #43843 ) ;
#17684=ADVANCED_FACE ( 'NONE', ( #134748 ), #111527, .F. ) ;
#17686=EDGE_CURVE ( 'NONE', #116862, #536, #110784, .T. ) ;
#17687=ORIENTED_EDGE ( 'NONE', *, *, #48645, .F. ) ;
#17688=VECTOR ( 'NONE', #127441, 1000.000000000000000 ) ;
#17690=FACE_OUTER_BOUND ( 'NONE', #29308, .T. ) ;
#17691=CARTESIAN_POINT ( 'NONE',  ( 29.29298673570674438, -21.74070752338405654, 4.999753212805219782 ) ) ;
#17692=CARTESIAN_POINT ( 'NONE',  ( 29.27718569542920335, -21.72500000000000142, 5.000000000000000000 ) ) ;
#17693=DIRECTION ( 'NONE',  ( -0.000000000000000000, -0.3543493200069152693, 0.9351131265310292928 ) ) ;
#17694=EDGE_LOOP ( 'NONE', ( #83042, #100580, #89247, #6553 ) ) ;
#17695=ORIENTED_EDGE ( 'NONE', *, *, #63152, .F. ) ;
#17697=PLANE ( 'NONE',  #132603 ) ;
#17698=CARTESIAN_POINT ( 'NONE',  ( 13.49999999999990408, 15.43112307739202294, 4.000000000000000000 ) ) ;
#17699=EDGE_LOOP ( 'NONE', ( #126975, #106689, #48299, #86374 ) ) ;
#17700=ORIENTED_EDGE ( 'NONE', *, *, #137466, .T. ) ;
#17701=CARTESIAN_POINT ( 'NONE',  ( -30.48921356237309510, -27.52281430457076894, 5.000000000000000000 ) ) ;
#17704=CARTESIAN_POINT ( 'NONE',  ( 34.49999999999976552, 4.464255608400454101, 4.994342998332159667 ) ) ;
#17706=FACE_BOUND ( 'NONE', #33151, .T. ) ;
#17708=CARTESIAN_POINT ( 'NONE',  ( -2.994519915287485734, 28.92564299267940342, 4.000000000000000000 ) ) ;
#17711=ORIENTED_EDGE ( 'NONE', *, *, #40487, .F. ) ;
#17714=VECTOR ( 'NONE', #103165, 1000.000000000000227 ) ;
#17715=ORIENTED_EDGE ( 'NONE', *, *, #26330, .T. ) ;
#17716=ORIENTED_EDGE ( 'NONE', *, *, #123364, .F. ) ;
#17718=VERTEX_POINT ( 'NONE', #112260 ) ;
#17719=VECTOR ( 'NONE', #135267, 1000.000000000000000 ) ;
#17720=DIRECTION ( 'NONE',  ( 1.000000000000000000, -0.000000000000000000, -0.000000000000000000 ) ) ;
#17721=VECTOR ( 'NONE', #72827, 1000.000000000000000 ) ;
#17722=DIRECTION ( 'NONE',  ( -1.000000000000000000, 0.000000000000000000, -0.000000000000000000 ) ) ;
#17723=LINE ( 'NONE', #138834, #114229 ) ;
#17724=ORIENTED_EDGE ( 'NONE', *, *, #100296, .F. ) ;
#17725=CARTESIAN_POINT ( 'NONE',  ( -29.99999999999979039, 13.93112307739203892, 4.000000000000000000 ) ) ;
#17726=CARTESIAN_POINT ( 'NONE',  ( 15.79289321881335084, -11.24070752338416845, 5.000000000000000000 ) ) ;
#17728=DIRECTION ( 'NONE',  ( 0.7071067811865487940, -0.7071067811865463515, 0.000000000000000000 ) ) ;
#17729=LINE ( 'NONE', #139578, #7569 ) ;
#17731=CARTESIAN_POINT ( 'NONE',  ( -21.48921356237309155, -27.52281430457070499, 5.000000000000000000 ) ) ;
#17732=EDGE_LOOP ( 'NONE', ( #76289, #14200, #90520, #117297 ) ) ;
#17733=DIRECTION ( 'NONE',  ( -0.000000000000000000, -0.3543493200069152693, 0.9351131265310292928 ) ) ;
#17734=DIRECTION ( 'NONE',  ( 0.7071067811865487940, 0.7071067811865463515, 0.000000000000000000 ) ) ;
#17736=ORIENTED_EDGE ( 'NONE', *, *, #122820, .F. ) ;
#17739=EDGE_CURVE ( 'NONE', #33310, #61158, #46319, .T. ) ;
#17740=EDGE_LOOP ( 'NONE', ( #34336, #14267, #122950, #59371 ) ) ;
#17742=VERTEX_POINT ( 'NONE', #25224 ) ;
#17744=EDGE_CURVE ( 'NONE', #45590, #13451, #57900, .T. ) ;
#17745=EDGE_CURVE ( 'NONE', #74597, #118741, #35442, .T. ) ;
#17746=VECTOR ( 'NONE', #75653, 1000.000000000000000 ) ;
#17749=ORIENTED_EDGE ( 'NONE', *, *, #6728, .T. ) ;
#17750=EDGE_CURVE ( 'NONE', #13173, #77699, #73869, .T. ) ;
#17751=CARTESIAN_POINT ( 'NONE',  ( 18.28838880452753202, -2.745211937670052560, 5.000000000000000000 ) ) ;
#17752=ORIENTED_EDGE ( 'NONE', *, *, #1300, .T. ) ;
#17753=CARTESIAN_POINT ( 'NONE',  ( -28.49999999999979750, 0.4311230773921762571, 4.000000000000000000 ) ) ;
#17754=VECTOR ( 'NONE', #3753, 1000.000000000000000 ) ;
#17756=LINE ( 'NONE', #139603, #100359 ) ;
#17757=EDGE_LOOP ( 'NONE', ( #11864, #80979, #71115, #42183 ) ) ;
#17758=VERTEX_POINT ( 'NONE', #47058 ) ;
#17759=CARTESIAN_POINT ( 'NONE',  ( -34.92500000000001137, -12.18334561358944335, 4.500000000000000888 ) ) ;
#17761=EDGE_CURVE ( 'NONE', #65062, #117371, #99946, .T. ) ;
#17763=DIRECTION ( 'NONE',  ( 0.7071067811865486830, -0.7071067811865464625, -0.000000000000000000 ) ) ;
#17765=ORIENTED_EDGE ( 'NONE', *, *, #38528, .T. ) ;
#17766=VERTEX_POINT ( 'NONE', #58645 ) ;
#17767=ORIENTED_EDGE ( 'NONE', *, *, #112539, .T. ) ;
#17768=CARTESIAN_POINT ( 'NONE',  ( 10.19018167574442124, -18.74070752338409207, 7.910009926591483165 ) ) ;
#17769=ADVANCED_FACE ( 'NONE', ( #36817 ), #22345, .F. ) ;
#17770=CARTESIAN_POINT ( 'NONE',  ( 0.000000000000000000, 21.72500000000000142, 4.500000000000000888 ) ) ;
#17771=PLANE ( 'NONE',  #70297 ) ;
#17772=CARTESIAN_POINT ( 'NONE',  ( 9.792893218813388145, 18.75929247661553489, 5.000000000000000000 ) ) ;
#17773=VERTEX_POINT ( 'NONE', #28092 ) ;
#17774=CARTESIAN_POINT ( 'NONE',  ( -8.671830600776409881, -12.74070752338415424, 4.000000000000000000 ) ) ;
#17775=ORIENTED_EDGE ( 'NONE', *, *, #22179, .T. ) ;
#17776=VECTOR ( 'NONE', #116003, 1000.000000000000000 ) ;
#17777=EDGE_CURVE ( 'NONE', #96318, #103184, #72358, .T. ) ;
#17778=CARTESIAN_POINT ( 'NONE',  ( -26.99451991528749417, 28.92564299267956685, 4.000000000000000000 ) ) ;
#17780=DIRECTION ( 'NONE',  ( -0.7071067811865487940, 0.7071067811865463515, -0.000000000000000000 ) ) ;
#17783=CARTESIAN_POINT ( 'NONE',  ( 23.20666063542136115, 21.75929247661548871, 4.998822639870701856 ) ) ;
#17786=ORIENTED_EDGE ( 'NONE', *, *, #101685, .T. ) ;
#17788=ORIENTED_EDGE ( 'NONE', *, *, #53348, .T. ) ;
#17789=LINE ( 'NONE', #63503, #57986 ) ;
#17793=CARTESIAN_POINT ( 'NONE',  ( -34.47516574401892342, -17.97193265888399694, 4.998110765256835286 ) ) ;
#17797=DIRECTION ( 'NONE',  ( -0.6830127018922180770, -0.6830127018922204085, -0.2588190451025213501 ) ) ;
#17798=EDGE_CURVE ( 'NONE', #132198, #36664, #60768, .T. ) ;
#17800=LINE ( 'NONE', #108359, #71962 ) ;
#17802=EDGE_CURVE ( 'NONE', #1490, #104227, #82482, .T. ) ;
#17803=CARTESIAN_POINT ( 'NONE',  ( 34.36246187583877543, 22.22500000000000142, 4.000000000000000000 ) ) ;
#17805=ORIENTED_EDGE ( 'NONE', *, *, #1235, .F. ) ;
#17806=PLANE ( 'NONE',  #40676 ) ;
#17807=EDGE_LOOP ( 'NONE', ( #120913, #41421, #27639, #115257 ) ) ;
#17809=ADVANCED_FACE ( 'NONE', ( #39704 ), #73058, .F. ) ;
#17810=LINE ( 'NONE', #62079, #34564 ) ;
#17811=DIRECTION ( 'NONE',  ( 0.7071067811865486830, -0.7071067811865464625, -0.000000000000000000 ) ) ;
#17812=ORIENTED_EDGE ( 'NONE', *, *, #36306, .F. ) ;
#17814=CARTESIAN_POINT ( 'NONE',  ( -24.47512612785031294, 14.25929247661557753, 9.797011795316580063 ) ) ;
#17815=ORIENTED_EDGE ( 'NONE', *, *, #25789, .F. ) ;
#17816=VERTEX_POINT ( 'NONE', #115767 ) ;
#17817=CARTESIAN_POINT ( 'NONE',  ( 22.49999999999984723, -16.91253812416058011, 4.000000000000000000 ) ) ;
#17818=DIRECTION ( 'NONE',  ( 0.7071067811865487940, 0.7071067811865463515, -0.000000000000000000 ) ) ;
#17819=CARTESIAN_POINT ( 'NONE',  ( 60.48921356237309510, -27.52281430457097500, 5.000000000000000000 ) ) ;
#17821=FACE_OUTER_BOUND ( 'NONE', #116099, .T. ) ;
#17822=LINE ( 'NONE', #114978, #55259 ) ;
#17823=ORIENTED_EDGE ( 'NONE', *, *, #20831, .F. ) ;
#17824=VECTOR ( 'NONE', #55380, 1000.000000000000000 ) ;
#17825=EDGE_CURVE ( 'NONE', #75708, #12022, #117211, .T. ) ;
#17827=CARTESIAN_POINT ( 'NONE',  ( 14.81601139373099585, 28.73617430169776910, 5.000000000000000000 ) ) ;
#17829=DIRECTION ( 'NONE',  ( -0.6830127018922180770, -0.6830127018922204085, -0.2588190451025213501 ) ) ;
#17830=ORIENTED_EDGE ( 'NONE', *, *, #69011, .T. ) ;
#17832=ORIENTED_EDGE ( 'NONE', *, *, #11576, .F. ) ;
#17834=DIRECTION ( 'NONE',  ( 0.7071067811865487940, -0.7071067811865463515, 0.000000000000000000 ) ) ;
#17835=LINE ( 'NONE', #16408, #109424 ) ;
#17836=DIRECTION ( 'NONE',  ( 0.3543493200069162685, -0.000000000000000000, -0.9351131265310288487 ) ) ;
#17837=ORIENTED_EDGE ( 'NONE', *, *, #72526, .F. ) ;
#17838=DIRECTION ( 'NONE',  ( 0.3543493200069162685, -0.000000000000000000, -0.9351131265310288487 ) ) ;
#17839=CARTESIAN_POINT ( 'NONE',  ( -9.328169399223465774, -0.7407075233842718154, 4.000000000000000000 ) ) ;
#17841=CARTESIAN_POINT ( 'NONE',  ( 30.18398860626900060, 28.73617430169808173, 5.000000000000000000 ) ) ;
#17842=EDGE_CURVE ( 'NONE', #15864, #9322, #114382, .T. ) ;
#17843=CARTESIAN_POINT ( 'NONE',  ( 28.49999999999979750, -8.947814304570737676, 5.000000000000000000 ) ) ;
#17846=CARTESIAN_POINT ( 'NONE',  ( -42.48921356237308800, -27.52281430457085065, 5.000000000000000000 ) ) ;
#17848=AXIS2_PLACEMENT_3D ( 'NONE', #93858, #106132, #14866 ) ;
#17849=VECTOR ( 'NONE', #43082, 1000.000000000000227 ) ;
#17850=EDGE_LOOP ( 'NONE', ( #101128, #9708, #76905, #64073 ) ) ;
#17852=ORIENTED_EDGE ( 'NONE', *, *, #38412, .T. ) ;
#17853=AXIS2_PLACEMENT_3D ( 'NONE', #54464, #120356, #34124 ) ;
#17855=ORIENTED_EDGE ( 'NONE', *, *, #56587, .T. ) ;
#17856=DIRECTION ( 'NONE',  ( -0.7071067811865486830, 0.7071067811865464625, 0.000000000000000000 ) ) ;
#17857=CARTESIAN_POINT ( 'NONE',  ( 20.88987624306225754, 8.854559187742358617, 4.414246686754478510 ) ) ;
#17858=CARTESIAN_POINT ( 'NONE',  ( 14.99999999999990230, 7.007997736742463957, -8.085015511992081017 ) ) ;
#17859=ORIENTED_EDGE ( 'NONE', *, *, #104038, .T. ) ;
#17860=LINE ( 'NONE', #28062, #21325 ) ;
#17861=DIRECTION ( 'NONE',  ( -0.7071067811865486830, -0.7071067811865464625, -0.000000000000000000 ) ) ;
#17862=ADVANCED_FACE ( 'NONE', ( #61476 ), #128137, .F. ) ;
#17863=ORIENTED_EDGE ( 'NONE', *, *, #123371, .T. ) ;
#17864=LINE ( 'NONE', #51970, #32810 ) ;
#17865=DIRECTION ( 'NONE',  ( -0.7071067811865487940, 0.7071067811865463515, -0.000000000000000000 ) ) ;
#17866=CARTESIAN_POINT ( 'NONE',  ( 11.99999999999992006, 12.25461709320621928, -10.07315571508694418 ) ) ;
#17867=ORIENTED_EDGE ( 'NONE', *, *, #33167, .F. ) ;
#17868=ORIENTED_EDGE ( 'NONE', *, *, #91884, .F. ) ;
#17869=EDGE_CURVE ( 'NONE', #112404, #50577, #6280, .T. ) ;
#17870=CARTESIAN_POINT ( 'NONE',  ( -0.7071067811865398012, 8.259292476615641476, 5.000000000000000000 ) ) ;
#17872=LINE ( 'NONE', #106306, #108994 ) ;
#17873=DIRECTION ( 'NONE',  ( -0.000000000000000000, 0.3543493200069153248, 0.9351131265310292928 ) ) ;
#17874=AXIS2_PLACEMENT_3D ( 'NONE', #90914, #135145, #16143 ) ;
#17875=CARTESIAN_POINT ( 'NONE',  ( 17.70025512860841488, -27.71228299555193786, 4.000000000000000000 ) ) ;
#17876=CARTESIAN_POINT ( 'NONE',  ( 42.48921356237308800, -27.52281430457085065, 5.000000000000000000 ) ) ;
#17877=ORIENTED_EDGE ( 'NONE', *, *, #89697, .T. ) ;
#17879=ORIENTED_EDGE ( 'NONE', *, *, #118971, .F. ) ;
#17881=EDGE_LOOP ( 'NONE', ( #41173, #113679, #90274, #94479 ) ) ;
#17882=VECTOR ( 'NONE', #57689, 1000.000000000000000 ) ;
#17883=DIRECTION ( 'NONE',  ( -0.7071067811865486830, -0.7071067811865464625, 0.000000000000000000 ) ) ;
#17885=ORIENTED_EDGE ( 'NONE', *, *, #3415, .F. ) ;
#17886=LINE ( 'NONE', #71605, #101561 ) ;
#17888=DIRECTION ( 'NONE',  ( 0.7071067811865486830, -0.7071067811865464625, -0.000000000000000000 ) ) ;
#17889=ADVANCED_FACE ( 'NONE', ( #126669 ), #26663, .T. ) ;
#17894=PLANE ( 'NONE',  #41972 ) ;
#17896=ORIENTED_EDGE ( 'NONE', *, *, #4547, .F. ) ;
#17897=EDGE_CURVE ( 'NONE', #142173, #101006, #38262, .T. ) ;
#17898=EDGE_CURVE ( 'NONE', #142746, #129157, #7001, .T. ) ;
#17899=DIRECTION ( 'NONE',  ( -0.7071067811865486830, 0.7071067811865464625, 0.000000000000000000 ) ) ;
#17902=ORIENTED_EDGE ( 'NONE', *, *, #137261, .T. ) ;
#17903=EDGE_CURVE ( 'NONE', #35767, #104436, #38965, .T. ) ;
#17904=ADVANCED_FACE ( 'NONE', ( #40418 ), #15054, .F. ) ;
#17905=FACE_OUTER_BOUND ( 'NONE', #123016, .T. ) ;
#17906=ADVANCED_FACE ( 'NONE', ( #115058 ), #75197, .F. ) ;
#17907=VECTOR ( 'NONE', #781, 1000.000000000000227 ) ;
#17909=DIRECTION ( 'NONE',  ( -0.000000000000000000, 0.000000000000000000, 1.000000000000000000 ) ) ;
#17910=EDGE_CURVE ( 'NONE', #25446, #13935, #108457, .T. ) ;
#17911=CARTESIAN_POINT ( 'NONE',  ( -78.48921356237309510, -27.52281430457109934, 5.000000000000000000 ) ) ;
#17912=CARTESIAN_POINT ( 'NONE',  ( -42.48921356237308800, -27.52281430457085065, 5.000000000000000000 ) ) ;
#17913=PLANE ( 'NONE',  #128623 ) ;
#17915=DIRECTION ( 'NONE',  ( -0.3543493200069162685, -0.000000000000000000, -0.9351131265310288487 ) ) ;
#17918=EDGE_CURVE ( 'NONE', #15815, #2157, #9138, .T. ) ;
#17919=ORIENTED_EDGE ( 'NONE', *, *, #92572, .T. ) ;
#17920=AXIS2_PLACEMENT_3D ( 'NONE', #88839, #20694, #77265 ) ;
#17925=LINE ( 'NONE', #45992, #100590 ) ;
#17926=ORIENTED_EDGE ( 'NONE', *, *, #53196, .T. ) ;
#17927=DIRECTION ( 'NONE',  ( 0.3543493200069162685, -0.000000000000000000, -0.9351131265310288487 ) ) ;
#17928=LINE ( 'NONE', #86092, #68647 ) ;
#17929=EDGE_CURVE ( 'NONE', #5604, #91707, #63609, .T. ) ;
#17930=VECTOR ( 'NONE', #102630, 1000.000000000000000 ) ;
#17931=DIRECTION ( 'NONE',  ( -0.7071067811865486830, -0.7071067811865464625, -0.000000000000000000 ) ) ;
#17932=LINE ( 'NONE', #109802, #78820 ) ;
#17934=VERTEX_POINT ( 'NONE', #96869 ) ;
#17936=EDGE_LOOP ( 'NONE', ( #81907, #105161, #79468 ) ) ;
#17937=EDGE_CURVE ( 'NONE', #104733, #2653, #141875, .T. ) ;
#17938=VECTOR ( 'NONE', #133315, 1000.000000000000227 ) ;
#17939=VECTOR ( 'NONE', #80328, 999.9999999999998863 ) ;
#17942=LINE ( 'NONE', #16530, #48282 ) ;
#17944=ORIENTED_EDGE ( 'NONE', *, *, #137694, .F. ) ;
#17946=VERTEX_POINT ( 'NONE', #107770 ) ;
#17947=CARTESIAN_POINT ( 'NONE',  ( 68.99451991528748351, 28.92564299267986172, 4.000000000000000000 ) ) ;
#17948=VECTOR ( 'NONE', #22306, 999.9999999999998863 ) ;
#17949=FACE_OUTER_BOUND ( 'NONE', #35751, .T. ) ;
#17950=CARTESIAN_POINT ( 'NONE',  ( -60.29974487139158867, -27.71228299555248142, 4.000000000000000000 ) ) ;
#17951=CARTESIAN_POINT ( 'NONE',  ( 42.48921356237308800, -27.52281430457085065, 5.000000000000000000 ) ) ;
#17952=PLANE ( 'NONE',  #131335 ) ;
#17953=PLANE ( 'NONE',  #136743 ) ;
#17955=FACE_OUTER_BOUND ( 'NONE', #3459, .T. ) ;
#17957=EDGE_CURVE ( 'NONE', #125874, #139670, #141118, .T. ) ;
#17959=DIRECTION ( 'NONE',  ( 0.6830127018922180770, -0.6830127018922204085, -0.2588190451025213501 ) ) ;
#17960=PLANE ( 'NONE',  #140227 ) ;
#17962=ADVANCED_FACE ( 'NONE', ( #8431 ), #99035, .F. ) ;
#17963=CARTESIAN_POINT ( 'NONE',  ( 34.11017322888187664, -22.22500000000000142, 4.785647885939352975 ) ) ;
#17964=CARTESIAN_POINT ( 'NONE',  ( 12.48921356237309155, -27.52281430457064104, 5.000000000000000000 ) ) ;
#17966=CARTESIAN_POINT ( 'NONE',  ( -34.92500000000001137, -8.028593703617126209, -6.464217593021346353 ) ) ;
#17967=CARTESIAN_POINT ( 'NONE',  ( 15.29974487139158867, -27.71228299555216879, 4.000000000000000000 ) ) ;
#17968=AXIS2_PLACEMENT_3D ( 'NONE', #27920, #115590, #6123 ) ;
#17969=ORIENTED_EDGE ( 'NONE', *, *, #48082, .T. ) ;
#17970=CARTESIAN_POINT ( 'NONE',  ( -75.29974487139158157, -27.71228299555258445, 4.000000000000000000 ) ) ;
#17971=ORIENTED_EDGE ( 'NONE', *, *, #53875, .T. ) ;
#17972=DIRECTION ( 'NONE',  ( -0.3543493200069162685, -0.000000000000000000, -0.9351131265310288487 ) ) ;
#17975=DIRECTION ( 'NONE',  ( 0.7071067811865486830, -0.7071067811865464625, -0.000000000000000000 ) ) ;
#17976=DIRECTION ( 'NONE',  ( 0.6830127018922180770, -0.6830127018922204085, -0.2588190451025213501 ) ) ;
#17977=EDGE_CURVE ( 'NONE', #110210, #138157, #42570, .T. ) ;
#17978=DIRECTION ( 'NONE',  ( 0.7071067811865487940, -0.7071067811865463515, 0.000000000000000000 ) ) ;
#17979=CARTESIAN_POINT ( 'NONE',  ( -14.99451991528749595, 28.92564299267948513, 4.000000000000000000 ) ) ;
#17983=CARTESIAN_POINT ( 'NONE',  ( -29.14994871458958414, -8.240707523384193323, 17.25253755692232360 ) ) ;
#17984=FACE_OUTER_BOUND ( 'NONE', #71363, .T. ) ;
#17985=CARTESIAN_POINT ( 'NONE',  ( 6.299744871391586898, -27.71228299555210484, 4.000000000000000000 ) ) ;
#17986=VERTEX_POINT ( 'NONE', #75887 ) ;
#17987=ORIENTED_EDGE ( 'NONE', *, *, #120981, .F. ) ;
#17989=FACE_OUTER_BOUND ( 'NONE', #95732, .T. ) ;
#17991=DIRECTION ( 'NONE',  ( 0.6830127018922180770, -0.6830127018922204085, -0.2588190451025213501 ) ) ;
#17993=CARTESIAN_POINT ( 'NONE',  ( 2.994519915287485734, 28.92564299267940342, 4.000000000000000000 ) ) ;
#17994=ORIENTED_EDGE ( 'NONE', *, *, #138838, .T. ) ;
#17995=DIRECTION ( 'NONE',  ( 0.6830127018922180770, -0.6830127018922204085, -0.2588190451025213501 ) ) ;
#17997=DIRECTION ( 'NONE',  ( -0.7071067811865486830, 0.7071067811865464625, 0.000000000000000000 ) ) ;
#17998=CARTESIAN_POINT ( 'NONE',  ( 11.99999999999993072, -16.44781430457065952, 5.000000000000000000 ) ) ;
#17999=EDGE_CURVE ( 'NONE', #68842, #925, #96175, .T. ) ;
#18001=ADVANCED_FACE ( 'NONE', ( #120052 ), #54861, .F. ) ;
#18002=CARTESIAN_POINT ( 'NONE',  ( 0.000000000000000000, 1.761378380278681099, -6.096875308897254264 ) ) ;
#18003=DIRECTION ( 'NONE',  ( 0.7071067811865486830, -0.7071067811865464625, -0.000000000000000000 ) ) ;
#18005=PLANE ( 'NONE',  #102598 ) ;
#18006=CARTESIAN_POINT ( 'NONE',  ( 29.99999999999979750, 4.384688058510596953, -7.090945410444616570 ) ) ;
#18007=DIRECTION ( 'NONE',  ( 0.7071067811865486830, -0.7071067811865464625, -0.000000000000000000 ) ) ;
#18009=EDGE_CURVE ( 'NONE', #27663, #125881, #143269, .T. ) ;
#18010=ORIENTED_EDGE ( 'NONE', *, *, #41523, .F. ) ;
#18013=VECTOR ( 'NONE', #49347, 1000.000000000000227 ) ;
#18015=EDGE_CURVE ( 'NONE', #23807, #3366, #119354, .T. ) ;
#18016=CARTESIAN_POINT ( 'NONE',  ( -1.499999999999987566, -10.53360074219763121, 5.000000000000000000 ) ) ;
#18017=CARTESIAN_POINT ( 'NONE',  ( -18.79289321881332242, -14.24070752338413648, 5.000000000000000000 ) ) ;
#18018=ORIENTED_EDGE ( 'NONE', *, *, #108113, .F. ) ;
#18020=DIRECTION ( 'NONE',  ( -0.000000000000000000, 0.000000000000000000, 1.000000000000000000 ) ) ;
#18023=EDGE_CURVE ( 'NONE', #7112, #55621, #32386, .T. ) ;
#18024=ORIENTED_EDGE ( 'NONE', *, *, #131323, .T. ) ;
#18025=CARTESIAN_POINT ( 'NONE',  ( 17.29298673570682254, -21.74070752338406720, 4.999753212805220670 ) ) ;
#18026=ORIENTED_EDGE ( 'NONE', *, *, #60411, .F. ) ;
#18027=LINE ( 'NONE', #52812, #1362 ) ;
#18028=DIRECTION ( 'NONE',  ( -0.000000000000000000, -0.000000000000000000, 1.000000000000000000 ) ) ;
#18029=AXIS2_PLACEMENT_3D ( 'NONE', #141734, #140979, #30836 ) ;
#18031=EDGE_LOOP ( 'NONE', ( #65134, #77199, #60960, #71114 ) ) ;
#18032=VERTEX_POINT ( 'NONE', #64294 ) ;
#18033=VECTOR ( 'NONE', #116338, 1000.000000000000000 ) ;
#18034=ORIENTED_EDGE ( 'NONE', *, *, #91827, .F. ) ;
#18035=DIRECTION ( 'NONE',  ( 0.7071067811865486830, -0.7071067811865464625, -0.000000000000000000 ) ) ;
#18036=EDGE_CURVE ( 'NONE', #37816, #67034, #7741, .T. ) ;
#18037=LINE ( 'NONE', #138441, #12965 ) ;
#18039=VECTOR ( 'NONE', #76263, 1000.000000000000227 ) ;
#18040=VECTOR ( 'NONE', #2941, 1000.000000000000000 ) ;
#18041=LINE ( 'NONE', #41250, #115001 ) ;
#18042=EDGE_LOOP ( 'NONE', ( #75263, #61863, #81232, #2864 ) ) ;
#18043=ORIENTED_EDGE ( 'NONE', *, *, #138932, .F. ) ;
#18044=DIRECTION ( 'NONE',  ( -0.7071067811865486830, -0.7071067811865464625, 0.000000000000000000 ) ) ;
#18045=VERTEX_POINT ( 'NONE', #84622 ) ;
#18046=ORIENTED_EDGE ( 'NONE', *, *, #13906, .T. ) ;
#18048=CARTESIAN_POINT ( 'NONE',  ( -28.49999999999979750, 3.073033219394599058, -6.593910359671034449 ) ) ;
#18049=VERTEX_POINT ( 'NONE', #41106 ) ;
#18050=DIRECTION ( 'NONE',  ( -0.7071067811865486830, 0.7071067811865464625, 0.000000000000000000 ) ) ;
#18051=EDGE_CURVE ( 'NONE', #43580, #104227, #128823, .T. ) ;
#18052=LINE ( 'NONE', #62341, #77980 ) ;
#18054=LINE ( 'NONE', #41267, #55994 ) ;
#18055=ORIENTED_EDGE ( 'NONE', *, *, #97627, .T. ) ;
#18056=AXIS2_PLACEMENT_3D ( 'NONE', #50288, #40829, #29929 ) ;
#18057=LINE ( 'NONE', #93527, #4639 ) ;
#18058=FACE_BOUND ( 'NONE', #12050, .T. ) ;
#18062=LINE ( 'NONE', #53609, #123316 ) ;
#18063=EDGE_CURVE ( 'NONE', #127570, #45162, #67907, .T. ) ;
#18064=EDGE_LOOP ( 'NONE', ( #113373, #102825, #55394, #5309 ) ) ;
#18065=CARTESIAN_POINT ( 'NONE',  ( 4.499999999999974243, 21.05218569542895679, 5.000000000000000000 ) ) ;
#18066=EDGE_LOOP ( 'NONE', ( #48211, #85871, #131204, #105891 ) ) ;
#18067=AXIS2_PLACEMENT_3D ( 'NONE', #44177, #65953, #78232 ) ;
#18068=VERTEX_POINT ( 'NONE', #126339 ) ;
#18069=EDGE_LOOP ( 'NONE', ( #80922, #85875, #82470, #19630 ) ) ;
#18070=ADVANCED_FACE ( 'NONE', ( #22187 ), #46132, .F. ) ;
#18072=LINE ( 'NONE', #126175, #52972 ) ;
#18073=LINE ( 'NONE', #52861, #31051 ) ;
#18074=ADVANCED_FACE ( 'NONE', ( #114728 ), #103840, .F. ) ;
#18075=LINE ( 'NONE', #61656, #46250 ) ;
#18076=CARTESIAN_POINT ( 'NONE',  ( 14.67183060077636725, 14.25929247661557042, 4.000000000000000000 ) ) ;
#18077=EDGE_CURVE ( 'NONE', #67478, #143446, #1829, .T. ) ;
#18078=DIRECTION ( 'NONE',  ( -0.000000000000000000, 0.3543493200069153248, 0.9351131265310292928 ) ) ;
#18079=DIRECTION ( 'NONE',  ( -0.000000000000000000, 0.000000000000000000, 1.000000000000000000 ) ) ;
#18080=VECTOR ( 'NONE', #24541, 1000.000000000000000 ) ;
#18082=DIRECTION ( 'NONE',  ( 0.7071067811865486830, -0.7071067811865464625, -0.000000000000000000 ) ) ;
#18083=CARTESIAN_POINT ( 'NONE',  ( -39.48921356237310221, -27.52281430457082934, 5.000000000000000000 ) ) ;
#18085=CARTESIAN_POINT ( 'NONE',  ( 13.84116387061258457, 6.089959206779446355, 4.000000000000000000 ) ) ;
#18086=EDGE_CURVE ( 'NONE', #22993, #21534, #16113, .T. ) ;
#18087=ORIENTED_EDGE ( 'NONE', *, *, #9508, .F. ) ;
#18088=VERTEX_POINT ( 'NONE', #82162 ) ;
#18089=EDGE_LOOP ( 'NONE', ( #77156, #46075, #75331, #4352 ) ) ;
#18090=ORIENTED_EDGE ( 'NONE', *, *, #86206, .T. ) ;
#18091=DIRECTION ( 'NONE',  ( 1.000000000000000000, 0.000000000000000000, 0.000000000000000000 ) ) ;
#18092=ORIENTED_EDGE ( 'NONE', *, *, #22680, .F. ) ;
#18094=CARTESIAN_POINT ( 'NONE',  ( -51.18398860626899705, 28.73617430169823095, 5.000000000000000000 ) ) ;
#18095=CARTESIAN_POINT ( 'NONE',  ( 0.000000000000000000, 0.000000000000000000, 5.000000000000000000 ) ) ;
#18096=DIRECTION ( 'NONE',  ( -0.3543493200069162685, -0.000000000000000000, -0.9351131265310288487 ) ) ;
#18098=ADVANCED_FACE ( 'NONE', ( #122217 ), #57014, .F. ) ;
#18099=DIRECTION ( 'NONE',  ( -0.6830127018922180770, -0.6830127018922204085, -0.2588190451025213501 ) ) ;
#18101=CARTESIAN_POINT ( 'NONE',  ( 24.21271579574130683, 0.1791150535437372460, 5.000000000000000000 ) ) ;
#18102=ORIENTED_EDGE ( 'NONE', *, *, #35864, .F. ) ;
#18103=EDGE_CURVE ( 'NONE', #84862, #129515, #67153, .T. ) ;
#18104=LINE ( 'NONE', #93572, #76861 ) ;
#18105=PLANE ( 'NONE',  #40379 ) ;
#18107=VERTEX_POINT ( 'NONE', #59682 ) ;
#18109=VECTOR ( 'NONE', #112453, 1000.000000000000227 ) ;
#18111=DIRECTION ( 'NONE',  ( 1.000000000000000000, 0.000000000000000000, 0.000000000000000000 ) ) ;
#18112=ORIENTED_EDGE ( 'NONE', *, *, #108895, .T. ) ;
#18113=ORIENTED_EDGE ( 'NONE', *, *, #39306, .F. ) ;
#18115=VERTEX_POINT ( 'NONE', #37191 ) ;
#18116=CARTESIAN_POINT ( 'NONE',  ( -21.18398860626899349, 28.73617430169802134, 5.000000000000000000 ) ) ;
#18117=CARTESIAN_POINT ( 'NONE',  ( -23.99451991528749062, 28.92564299267954908, 4.000000000000000000 ) ) ;
#18118=DIRECTION ( 'NONE',  ( -0.7071067811865486830, -0.7071067811865463515, 0.000000000000000000 ) ) ;
#18119=CARTESIAN_POINT ( 'NONE',  ( -23.99999999999982592, -22.22500000000000853, 4.412002311790067743 ) ) ;
#18121=VERTEX_POINT ( 'NONE', #4491 ) ;
#18122=DIRECTION ( 'NONE',  ( 0.7071067811865486830, -0.7071067811865464625, -0.000000000000000000 ) ) ;
#18123=AXIS2_PLACEMENT_3D ( 'NONE', #22580, #68314, #92139 ) ;
#18124=CARTESIAN_POINT ( 'NONE',  ( -8.994519915287490619, 28.92564299267944250, 4.000000000000000000 ) ) ;
#18126=ADVANCED_FACE ( 'NONE', ( #122958 ), #88925, .T. ) ;
#18127=ORIENTED_EDGE ( 'NONE', *, *, #34084, .F. ) ;
#18128=CARTESIAN_POINT ( 'NONE',  ( 34.49999999999975131, -5.945670655168991736, 4.994342998332164996 ) ) ;
#18129=VECTOR ( 'NONE', #55027, 1000.000000000000000 ) ;
#18132=ORIENTED_EDGE ( 'NONE', *, *, #49739, .T. ) ;
#18133=VECTOR ( 'NONE', #10236, 1000.000000000000000 ) ;
#18134=DIRECTION ( 'NONE',  ( -0.6830127018922180770, -0.6830127018922204085, -0.2588190451025213501 ) ) ;
#18136=AXIS2_PLACEMENT_3D ( 'NONE', #17951, #19413, #94805 ) ;
#18137=CARTESIAN_POINT ( 'NONE',  ( -34.92500000000001137, 12.95788372223792528, 1.488343219358023939 ) ) ;
#18138=LINE ( 'NONE', #106581, #62295 ) ;
#18139=VECTOR ( 'NONE', #50761, 1000.000000000000000 ) ;
#18140=ORIENTED_EDGE ( 'NONE', *, *, #110779, .F. ) ;
#18141=FACE_OUTER_BOUND ( 'NONE', #94402, .T. ) ;
#18142=VECTOR ( 'NONE', #29226, 999.9999999999998863 ) ;
#18143=EDGE_CURVE ( 'NONE', #75982, #108304, #111343, .T. ) ;
#18144=LINE ( 'NONE', #105877, #70683 ) ;
#18146=DIRECTION ( 'NONE',  ( 0.7071067811865487940, -0.7071067811865463515, 0.000000000000000000 ) ) ;
#18147=CARTESIAN_POINT ( 'NONE',  ( -36.48921356237310221, -27.52281430457080802, 5.000000000000000000 ) ) ;
#18149=DIRECTION ( 'NONE',  ( 0.3543493200069162685, -0.000000000000000000, -0.9351131265310288487 ) ) ;
#18150=DIRECTION ( 'NONE',  ( 0.7071067811865487940, 0.7071067811865463515, -0.000000000000000000 ) ) ;
#18151=DIRECTION ( 'NONE',  ( 0.6830127018922180770, -0.6830127018922204085, -0.2588190451025213501 ) ) ;
#18152=DIRECTION ( 'NONE',  ( -0.7071067811865487940, 0.7071067811865463515, 0.000000000000000000 ) ) ;
#18153=CARTESIAN_POINT ( 'NONE',  ( -17.99451991528748351, 28.92564299267950645, 4.000000000000000000 ) ) ;
#18154=CARTESIAN_POINT ( 'NONE',  ( 8.999999999999944933, 4.384688058510572972, -7.090945410444662755 ) ) ;
#18155=CARTESIAN_POINT ( 'NONE',  ( 23.20710678118638626, -14.24070752338414536, 5.000000000000000000 ) ) ;
#18156=VERTEX_POINT ( 'NONE', #71269 ) ;
#18157=ORIENTED_EDGE ( 'NONE', *, *, #50372, .F. ) ;
#18158=ORIENTED_EDGE ( 'NONE', *, *, #76231, .T. ) ;
#18161=EDGE_LOOP ( 'NONE', ( #8393, #125638, #63101, #142791 ) ) ;
#18162=EDGE_LOOP ( 'NONE', ( #12291, #124677, #5086, #62056 ) ) ;
#18163=ADVANCED_FACE ( 'NONE', ( #104588 ), #56319, .F. ) ;
#18164=ORIENTED_EDGE ( 'NONE', *, *, #98814, .T. ) ;
#18165=CARTESIAN_POINT ( 'NONE',  ( 47.99451991528749062, 28.92564299267971251, 4.000000000000000000 ) ) ;
#18166=VECTOR ( 'NONE', #127500, 1000.000000000000000 ) ;
#18167=LINE ( 'NONE', #5152, #141216 ) ;
#18168=VERTEX_POINT ( 'NONE', #100499 ) ;
#18169=DIRECTION ( 'NONE',  ( 0.7071067811865487940, 0.7071067811865463515, 0.000000000000000000 ) ) ;
#18172=DIRECTION ( 'NONE',  ( -0.6830127018922181881, 0.6830127018922202975, -0.2588190451025214056 ) ) ;
#18173=DIRECTION ( 'NONE',  ( 0.6830127018922180770, -0.6830127018922204085, -0.2588190451025213501 ) ) ;
#18175=EDGE_CURVE ( 'NONE', #19828, #13154, #23636, .T. ) ;
#18176=EDGE_LOOP ( 'NONE', ( #132395, #53154, #114863, #72607 ) ) ;
#18177=DIRECTION ( 'NONE',  ( -0.7071067811865486830, 0.7071067811865464625, 0.000000000000000000 ) ) ;
#18181=VECTOR ( 'NONE', #73832, 1000.000000000000000 ) ;
#18182=DIRECTION ( 'NONE',  ( -0.7071067811865486830, -0.7071067811865464625, 0.000000000000000000 ) ) ;
#18183=FACE_OUTER_BOUND ( 'NONE', #38565, .T. ) ;
#18185=LINE ( 'NONE', #8721, #104600 ) ;
#18186=CARTESIAN_POINT ( 'NONE',  ( -34.92500000000001137, 22.22500000000000142, 4.000000000000000000 ) ) ;
#18187=EDGE_LOOP ( 'NONE', ( #136546, #105778, #124315, #83485 ) ) ;
#18188=ORIENTED_EDGE ( 'NONE', *, *, #108773, .T. ) ;
#18190=ORIENTED_EDGE ( 'NONE', *, *, #120509, .F. ) ;
#18191=DIRECTION ( 'NONE',  ( -0.7071067811865486830, -0.7071067811865464625, -0.000000000000000000 ) ) ;
#18192=LINE ( 'NONE', #105928, #57074 ) ;
#18193=VECTOR ( 'NONE', #109810, 1000.000000000000000 ) ;
#18194=DIRECTION ( 'NONE',  ( -0.000000000000000000, 0.000000000000000000, 1.000000000000000000 ) ) ;
#18195=EDGE_CURVE ( 'NONE', #121192, #69181, #40085, .T. ) ;
#18196=PLANE ( 'NONE',  #16820 ) ;
#18197=VECTOR ( 'NONE', #119787, 1000.000000000000000 ) ;
#18198=LINE ( 'NONE', #129854, #7330 ) ;
#18201=ADVANCED_FACE ( 'NONE', ( #83575 ), #95848, .F. ) ;
#18202=EDGE_LOOP ( 'NONE', ( #24361, #32154, #113453, #103706 ) ) ;
#18204=ORIENTED_EDGE ( 'NONE', *, *, #61364, .T. ) ;
#18205=DIRECTION ( 'NONE',  ( -0.7071067811865486830, -0.7071067811865464625, -0.000000000000000000 ) ) ;
#18207=DIRECTION ( 'NONE',  ( 0.7071067811865487940, 0.7071067811865463515, -0.000000000000000000 ) ) ;
#18208=LINE ( 'NONE', #63909, #85754 ) ;
#18209=EDGE_LOOP ( 'NONE', ( #56222, #52445, #107958, #69287 ) ) ;
#18210=EDGE_CURVE ( 'NONE', #139467, #115804, #61148, .T. ) ;
#18212=ORIENTED_EDGE ( 'NONE', *, *, #131358, .F. ) ;
#18213=DIRECTION ( 'NONE',  ( -0.000000000000000000, 0.000000000000000000, 1.000000000000000000 ) ) ;
#18215=PLANE ( 'NONE',  #11442 ) ;
#18216=CARTESIAN_POINT ( 'NONE',  ( -34.92500000000001137, 10.51246187583939395, 4.000000000000000000 ) ) ;
#18217=CARTESIAN_POINT ( 'NONE',  ( 31.36246187583879674, 22.22500000000000142, 4.000000000000000000 ) ) ;
#18220=ORIENTED_EDGE ( 'NONE', *, *, #121798, .F. ) ;
#18221=CARTESIAN_POINT ( 'NONE',  ( 1.171830600776465392, 9.759292476615627265, 4.000000000000000000 ) ) ;
#18222=PLANE ( 'NONE',  #110371 ) ;
#18223=ORIENTED_EDGE ( 'NONE', *, *, #6618, .T. ) ;
#18224=ORIENTED_EDGE ( 'NONE', *, *, #119546, .T. ) ;
#18225=ORIENTED_EDGE ( 'NONE', *, *, #114224, .T. ) ;
#18227=AXIS2_PLACEMENT_3D ( 'NONE', #61013, #94290, #131213 ) ;
#18228=LINE ( 'NONE', #115394, #56104 ) ;
#18229=ORIENTED_EDGE ( 'NONE', *, *, #4194, .T. ) ;
#18231=VECTOR ( 'NONE', #114209, 999.9999999999998863 ) ;
#18234=DIRECTION ( 'NONE',  ( -0.7071067811865487940, 0.7071067811865463515, -0.000000000000000000 ) ) ;
#18235=AXIS2_PLACEMENT_3D ( 'NONE', #131148, #23061, #142737 ) ;
#18236=FACE_BOUND ( 'NONE', #26236, .T. ) ;
#18237=LINE ( 'NONE', #62519, #82742 ) ;
#18238=CARTESIAN_POINT ( 'NONE',  ( 23.99999999999983302, -9.412538124160661823, 4.000000000000000000 ) ) ;
#18239=CARTESIAN_POINT ( 'NONE',  ( -8.816011393731004731, 28.73617430169781173, 5.000000000000000000 ) ) ;
#18240=ORIENTED_EDGE ( 'NONE', *, *, #74596, .F. ) ;
#18241=PLANE ( 'NONE',  #22600 ) ;
#18242=ORIENTED_EDGE ( 'NONE', *, *, #27836, .F. ) ;
#18243=ORIENTED_EDGE ( 'NONE', *, *, #59968, .F. ) ;
#18247=EDGE_LOOP ( 'NONE', ( #16706, #21337, #88581, #70164 ) ) ;
#18250=ORIENTED_EDGE ( 'NONE', *, *, #135892, .T. ) ;
#18251=CARTESIAN_POINT ( 'NONE',  ( -69.48921356237309510, -27.52281430457103895, 5.000000000000000000 ) ) ;
#18252=ADVANCED_FACE ( 'NONE', ( #85674 ), #28475, .F. ) ;
#18253=CARTESIAN_POINT ( 'NONE',  ( -14.99999999999988987, -12.41253812416063163, 4.000000000000000000 ) ) ;
#18254=ORIENTED_EDGE ( 'NONE', *, *, #59434, .T. ) ;
#18255=CARTESIAN_POINT ( 'NONE',  ( 15.18398860626900237, 28.73617430169797871, 5.000000000000000000 ) ) ;
#18256=AXIS2_PLACEMENT_3D ( 'NONE', #42814, #74733, #142816 ) ;
#18257=EDGE_CURVE ( 'NONE', #88566, #52144, #30619, .T. ) ;
#18258=EDGE_CURVE ( 'NONE', #136293, #131560, #63269, .T. ) ;
#18259=VECTOR ( 'NONE', #32313, 1000.000000000000000 ) ;
#18260=DIRECTION ( 'NONE',  ( -0.7071067811865487940, 0.7071067811865463515, 0.000000000000000000 ) ) ;
#18261=PLANE ( 'NONE',  #94510 ) ;
#18262=LINE ( 'NONE', #106709, #18039 ) ;
#18263=LINE ( 'NONE', #48807, #90926 ) ;
#18264=CARTESIAN_POINT ( 'NONE',  ( 23.70025512860841133, -27.71228299555189523, 4.000000000000000000 ) ) ;
#18265=ORIENTED_EDGE ( 'NONE', *, *, #106262, .F. ) ;
#18266=VERTEX_POINT ( 'NONE', #18253 ) ;
#18269=DIRECTION ( 'NONE',  ( 0.6830127018922180770, -0.6830127018922204085, -0.2588190451025213501 ) ) ;
#18270=VERTEX_POINT ( 'NONE', #96530 ) ;
#18271=AXIS2_PLACEMENT_3D ( 'NONE', #131605, #76526, #120701 ) ;
#18272=ORIENTED_EDGE ( 'NONE', *, *, #126773, .F. ) ;
#18274=ORIENTED_EDGE ( 'NONE', *, *, #13215, .T. ) ;
#18275=CARTESIAN_POINT ( 'NONE',  ( -30.48921356237309510, -27.52281430457076894, 5.000000000000000000 ) ) ;
#18276=EDGE_CURVE ( 'NONE', #16863, #129679, #119025, .T. ) ;
#18277=EDGE_CURVE ( 'NONE', #129125, #25409, #116889, .T. ) ;
#18278=FACE_OUTER_BOUND ( 'NONE', #63053, .T. ) ;
#18279=VERTEX_POINT ( 'NONE', #62533 ) ;
#18280=VECTOR ( 'NONE', #79602, 1000.000000000000000 ) ;
#18281=CARTESIAN_POINT ( 'NONE',  ( 41.99451991528749062, 28.92564299267967343, 4.000000000000000000 ) ) ;
#18283=ADVANCED_FACE ( 'NONE', ( #140095 ), #49535, .F. ) ;
#18285=LINE ( 'NONE', #51681, #28710 ) ;
#18289=DIRECTION ( 'NONE',  ( -0.7071067811865486830, -0.7071067811865464625, 0.000000000000000000 ) ) ;
#18290=ADVANCED_FACE ( 'NONE', ( #39356 ), #129180, .F. ) ;
#18291=VECTOR ( 'NONE', #34228, 1000.000000000000000 ) ;
#18293=VERTEX_POINT ( 'NONE', #72737 ) ;
#18295=EDGE_LOOP ( 'NONE', ( #88554, #101503, #21158 ) ) ;
#18299=ORIENTED_EDGE ( 'NONE', *, *, #115303, .T. ) ;
#18300=DIRECTION ( 'NONE',  ( -0.6830127018922181881, 0.6830127018922202975, -0.2588190451025214056 ) ) ;
#18301=CARTESIAN_POINT ( 'NONE',  ( 10.40832548098994614, -0.7407075233842770334, 14.76736230305383124 ) ) ;
#18302=FACE_OUTER_BOUND ( 'NONE', #27934, .T. ) ;
#18303=EDGE_CURVE ( 'NONE', #121955, #110155, #118300, .T. ) ;
#18304=ORIENTED_EDGE ( 'NONE', *, *, #53359, .T. ) ;
#18305=CARTESIAN_POINT ( 'NONE',  ( 7.499999999999944045, -1.592773361805365662, -6.492772025301245087 ) ) ;
#18306=CARTESIAN_POINT ( 'NONE',  ( 29.99999999999979750, 7.007997736742478168, -8.085015511992047266 ) ) ;
#18307=DIRECTION ( 'NONE',  ( -0.7071067811865486830, -0.7071067811865464625, 0.000000000000000000 ) ) ;
#18308=LINE ( 'NONE', #108891, #70397 ) ;
#18310=ORIENTED_EDGE ( 'NONE', *, *, #91077, .T. ) ;
#18312=DIRECTION ( 'NONE',  ( -0.3543493200069162685, -0.000000000000000000, -0.9351131265310288487 ) ) ;
#18313=CARTESIAN_POINT ( 'NONE',  ( 0.000000000000000000, 0.000000000000000000, 5.000000000000000000 ) ) ;
#18314=EDGE_CURVE ( 'NONE', #22706, #83800, #52342, .T. ) ;
#18316=DIRECTION ( 'NONE',  ( 1.000000000000000000, 0.000000000000000000, 0.000000000000000000 ) ) ;
#18317=LINE ( 'NONE', #118367, #41349 ) ;
#18318=FACE_OUTER_BOUND ( 'NONE', #126621, .T. ) ;
#18323=CARTESIAN_POINT ( 'NONE',  ( 0.4892135623730947680, -27.52281430457055578, 5.000000000000000000 ) ) ;
#18325=DIRECTION ( 'NONE',  ( 0.7071067811865486830, -0.7071067811865464625, -0.000000000000000000 ) ) ;
#18326=ORIENTED_EDGE ( 'NONE', *, *, #138877, .T. ) ;
#18327=DIRECTION ( 'NONE',  ( -0.000000000000000000, 0.3543493200069153248, 0.9351131265310292928 ) ) ;
#18328=VECTOR ( 'NONE', #129059, 999.9999999999998863 ) ;
#18329=EDGE_LOOP ( 'NONE', ( #112922, #130805, #85876, #7050 ) ) ;
#18330=ADVANCED_FACE ( 'NONE', ( #137950 ), #38627, .F. ) ;
#18332=FACE_OUTER_BOUND ( 'NONE', #65457, .T. ) ;
#18333=VECTOR ( 'NONE', #71099, 1000.000000000000000 ) ;
#18334=VECTOR ( 'NONE', #3188, 1000.000000000000000 ) ;
#18336=LINE ( 'NONE', #39440, #99408 ) ;
#18337=LINE ( 'NONE', #61910, #2506 ) ;
#18338=VECTOR ( 'NONE', #39707, 1000.000000000000000 ) ;
#18339=CARTESIAN_POINT ( 'NONE',  ( 27.79333936457828358, 21.75929247661549226, 4.998822639870708073 ) ) ;
#18341=CARTESIAN_POINT ( 'NONE',  ( 30.18398860626900060, 28.73617430169808173, 5.000000000000000000 ) ) ;
#18342=EDGE_CURVE ( 'NONE', #28284, #56879, #132069, .T. ) ;
#18343=ORIENTED_EDGE ( 'NONE', *, *, #118922, .T. ) ;
#18344=CARTESIAN_POINT ( 'NONE',  ( -31.49999999999977973, 16.18958161055400069, -11.56426086740818704 ) ) ;
#18345=DIRECTION ( 'NONE',  ( -0.6830127018922181881, 0.6830127018922202975, -0.2588190451025214056 ) ) ;
#18346=CARTESIAN_POINT ( 'NONE',  ( 7.689442160698723328, -22.22500000000000142, 21.14820514618944713 ) ) ;
#18347=VECTOR ( 'NONE', #3536, 1000.000000000000000 ) ;
#18348=DIRECTION ( 'NONE',  ( 1.000000000000000000, 0.000000000000000000, 0.000000000000000000 ) ) ;
#18349=DIRECTION ( 'NONE',  ( -0.6830127018922181881, 0.6830127018922202975, -0.2588190451025214056 ) ) ;
#18350=DIRECTION ( 'NONE',  ( -0.6830127018922181881, 0.6830127018922202975, -0.2588190451025214056 ) ) ;
#18352=PLANE ( 'NONE',  #94744 ) ;
#18353=EDGE_LOOP ( 'NONE', ( #5985, #68071, #143528, #6752 ) ) ;
#18354=EDGE_LOOP ( 'NONE', ( #49112, #69125, #113431, #111599 ) ) ;
#18355=( BOUNDED_CURVE ( )  B_SPLINE_CURVE ( 3, ( #13439, #125082, #122210, #78036 ),
 .UNSPECIFIED., .F., .T. ) 
 B_SPLINE_CURVE_WITH_KNOTS ( ( 4, 4 ),
 ( 1.864375635226952044, 1.933014472006561624 ),
 .UNSPECIFIED. ) 
 CURVE ( )  GEOMETRIC_REPRESENTATION_ITEM ( )  RATIONAL_B_SPLINE_CURVE ( ( 1.000000000000000000, 0.9996074310407765395, 0.9996074310407765395, 1.000000000000000000 ) ) 
 REPRESENTATION_ITEM ( '' )  );
#18357=CARTESIAN_POINT ( 'NONE',  ( -32.20710678118632586, 9.759292476615627265, 5.000000000000000000 ) ) ;
#18358=CARTESIAN_POINT ( 'NONE',  ( -23.99999999999982592, 19.55218569542896390, 5.000000000000000000 ) ) ;
#18359=VECTOR ( 'NONE', #73129, 1000.000000000000000 ) ;
#18362=ORIENTED_EDGE ( 'NONE', *, *, #21080, .T. ) ;
#18364=AXIS2_PLACEMENT_3D ( 'NONE', #126971, #115353, #39282 ) ;
#18366=ADVANCED_FACE ( 'NONE', ( #110271 ), #33485, .F. ) ;
#18367=VERTEX_POINT ( 'NONE', #131339 ) ;
#18368=ADVANCED_FACE ( 'NONE', ( #122585 ), #45089, .F. ) ;
#18369=CARTESIAN_POINT ( 'NONE',  ( 11.99999999999991651, 4.931123077392129517, 4.000000000000000000 ) ) ;
#18370=ORIENTED_EDGE ( 'NONE', *, *, #134582, .T. ) ;
#18372=DIRECTION ( 'NONE',  ( -0.6830127018922180770, -0.6830127018922204085, -0.2588190451025213501 ) ) ;
#18373=VECTOR ( 'NONE', #13946, 1000.000000000000000 ) ;
#18374=VECTOR ( 'NONE', #70506, 1000.000000000000000 ) ;
#18375=LINE ( 'NONE', #82268, #121760 ) ;
#18376=LINE ( 'NONE', #19127, #14232 ) ;
#18377=AXIS2_PLACEMENT_3D ( 'NONE', #139286, #39978, #128390 ) ;
#18378=FACE_OUTER_BOUND ( 'NONE', #107432, .T. ) ;
#18380=CARTESIAN_POINT ( 'NONE',  ( -3.758600742197928835, 21.72499999999999432, 5.000000000000000000 ) ) ;
#18382=ORIENTED_EDGE ( 'NONE', *, *, #19594, .T. ) ;
#18384=DIRECTION ( 'NONE',  ( -0.7071067811865487940, 0.7071067811865463515, 0.000000000000000000 ) ) ;
#18385=DIRECTION ( 'NONE',  ( 0.7071067811865487940, 0.7071067811865463515, 0.000000000000000000 ) ) ;
#18387=AXIS2_PLACEMENT_3D ( 'NONE', #54615, #32131, #98798 ) ;
#18388=CARTESIAN_POINT ( 'NONE',  ( 6.299744871391586898, -27.71228299555210484, 4.000000000000000000 ) ) ;
#18389=DIRECTION ( 'NONE',  ( -4.681814790819591790E-17, -0.3543493200069152693, 0.9351131265310292928 ) ) ;
#18390=VERTEX_POINT ( 'NONE', #66798 ) ;
#18392=EDGE_CURVE ( 'NONE', #72085, #14802, #86425, .T. ) ;
#18393=CARTESIAN_POINT ( 'NONE',  ( 0.000000000000000000, 0.000000000000000000, 5.000000000000000000 ) ) ;
#18395=DIRECTION ( 'NONE',  ( 0.7071067811865487940, 0.7071067811865463515, 0.000000000000000000 ) ) ;
#18396=LINE ( 'NONE', #119163, #1496 ) ;
#18397=DIRECTION ( 'NONE',  ( 0.7071067811865487940, 0.7071067811865463515, -0.000000000000000000 ) ) ;
#18398=VERTEX_POINT ( 'NONE', #97241 ) ;
#18399=VERTEX_POINT ( 'NONE', #130651 ) ;
#18401=CARTESIAN_POINT ( 'NONE',  ( 29.67183060077626067, -15.74070752338412760, 4.000000000000000000 ) ) ;
#18403=ORIENTED_EDGE ( 'NONE', *, *, #103890, .T. ) ;
#18404=ADVANCED_FACE ( 'NONE', ( #66101 ), #121160, .T. ) ;
#18405=VERTEX_POINT ( 'NONE', #75541 ) ;
#18406=DIRECTION ( 'NONE',  ( -0.7071067811865487940, 0.7071067811865463515, -0.000000000000000000 ) ) ;
#18407=ORIENTED_EDGE ( 'NONE', *, *, #46115, .T. ) ;
#18408=CARTESIAN_POINT ( 'NONE',  ( 25.49999999999982236, 19.39370406404969316, 1.459788787078142303 ) ) ;
#18409=DIRECTION ( 'NONE',  ( 0.7071067811865486830, -0.7071067811865464625, -0.000000000000000000 ) ) ;
#18410=FACE_BOUND ( 'NONE', #67679, .T. ) ;
#18411=CARTESIAN_POINT ( 'NONE',  ( 32.99999999999977973, -9.412538124160656494, 4.000000000000000000 ) ) ;
#18413=CARTESIAN_POINT ( 'NONE',  ( 8.510786437626906675, -27.52281430457049183, 5.000000000000000000 ) ) ;
#18414=LINE ( 'NONE', #62694, #117586 ) ;
#18415=VERTEX_POINT ( 'NONE', #55211 ) ;
#18416=( BOUNDED_CURVE ( )  B_SPLINE_CURVE ( 3, ( #99650, #64195, #10497, #53295 ),
 .UNSPECIFIED., .F., .T. ) 
 B_SPLINE_CURVE_WITH_KNOTS ( ( 4, 4 ),
 ( 4.767201131347619025, 4.812229608965456151 ),
 .UNSPECIFIED. ) 
 CURVE ( )  GEOMETRIC_REPRESENTATION_ITEM ( )  RATIONAL_B_SPLINE_CURVE ( ( 1.000000000000000000, 0.9998310434873430852, 0.9998310434873430852, 1.000000000000000000 ) ) 
 REPRESENTATION_ITEM ( '' )  );
#18417=EDGE_LOOP ( 'NONE', ( #103564, #51985, #42721, #1579 ) ) ;
#18418=EDGE_CURVE ( 'NONE', #38637, #70950, #119712, .T. ) ;
#18419=VERTEX_POINT ( 'NONE', #120415 ) ;
#18421=ORIENTED_EDGE ( 'NONE', *, *, #120728, .T. ) ;
#18422=DIRECTION ( 'NONE',  ( -0.000000000000000000, 0.000000000000000000, 1.000000000000000000 ) ) ;
#18423=PLANE ( 'NONE',  #132254 ) ;
#18424=EDGE_CURVE ( 'NONE', #46586, #46174, #98001, .T. ) ;
#18425=CARTESIAN_POINT ( 'NONE',  ( 13.03163515922184423, 2.259292476615701428, 13.77329220150640054 ) ) ;
#18427=EDGE_CURVE ( 'NONE', #49695, #373, #125466, .T. ) ;
#18428=DIRECTION ( 'NONE',  ( 1.000000000000000000, 0.000000000000000000, 0.000000000000000000 ) ) ;
#18429=DIRECTION ( 'NONE',  ( 0.3543493200069162685, -0.000000000000000000, -0.9351131265310288487 ) ) ;
#18431=DIRECTION ( 'NONE',  ( -0.000000000000000000, -0.3543493200069152693, 0.9351131265310292928 ) ) ;
#18432=VECTOR ( 'NONE', #94028, 1000.000000000000000 ) ;
#18433=VECTOR ( 'NONE', #86273, 1000.000000000000000 ) ;
#18434=CARTESIAN_POINT ( 'NONE',  ( 24.48921356237309510, -27.52281430457072631, 5.000000000000000000 ) ) ;
#18435=AXIS2_PLACEMENT_3D ( 'NONE', #40807, #32803, #98730 ) ;
#18436=EDGE_LOOP ( 'NONE', ( #68390, #99532, #56884, #141834 ) ) ;
#18437=EDGE_CURVE ( 'NONE', #30706, #36198, #3632, .T. ) ;
#18438=PLANE ( 'NONE',  #105085 ) ;
#18439=PLANE ( 'NONE',  #132225 ) ;
#18440=VECTOR ( 'NONE', #73414, 1000.000000000000000 ) ;
#18441=ORIENTED_EDGE ( 'NONE', *, *, #8726, .F. ) ;
#18442=VERTEX_POINT ( 'NONE', #68964 ) ;
#18444=EDGE_CURVE ( 'NONE', #109300, #99727, #2949, .T. ) ;
#18447=ORIENTED_EDGE ( 'NONE', *, *, #97526, .F. ) ;
#18448=AXIS2_PLACEMENT_3D ( 'NONE', #140344, #64944, #130922 ) ;
#18449=LINE ( 'NONE', #42414, #115770 ) ;
#18450=EDGE_CURVE ( 'NONE', #76165, #15535, #58834, .T. ) ;
#18451=AXIS2_PLACEMENT_3D ( 'NONE', #51706, #60456, #138715 ) ;
#18456=CARTESIAN_POINT ( 'NONE',  ( -45.18398860626900415, 28.73617430169818832, 5.000000000000000000 ) ) ;
#18457=VERTEX_POINT ( 'NONE', #92095 ) ;
#18458=LINE ( 'NONE', #138144, #7045 ) ;
#18459=VECTOR ( 'NONE', #93637, 1000.000000000000000 ) ;
#18460=DIRECTION ( 'NONE',  ( -0.000000000000000000, 0.000000000000000000, -1.000000000000000000 ) ) ;
#18461=ADVANCED_FACE ( 'NONE', ( #12398 ), #2204, .F. ) ;
#18462=CARTESIAN_POINT ( 'NONE',  ( -5.510786437626906675, -27.52281430457051314, 5.000000000000000000 ) ) ;
#18463=ORIENTED_EDGE ( 'NONE', *, *, #126914, .T. ) ;
#18464=ORIENTED_EDGE ( 'NONE', *, *, #78698, .F. ) ;
#18465=LINE ( 'NONE', #86639, #9866 ) ;
#18466=EDGE_LOOP ( 'NONE', ( #63622, #45031, #122439, #117856 ) ) ;
#18467=VECTOR ( 'NONE', #64972, 999.9999999999998863 ) ;
#18468=CARTESIAN_POINT ( 'NONE',  ( -0.1839886062690032631, 28.73617430169787568, 5.000000000000000000 ) ) ;
#18469=ORIENTED_EDGE ( 'NONE', *, *, #76575, .F. ) ;
#18471=ORIENTED_EDGE ( 'NONE', *, *, #47808, .F. ) ;
#18472=ORIENTED_EDGE ( 'NONE', *, *, #119317, .T. ) ;
#18473=DIRECTION ( 'NONE',  ( 0.7071067811865486830, -0.7071067811865464625, -0.000000000000000000 ) ) ;
#18474=EDGE_CURVE ( 'NONE', #140592, #80880, #69682, .T. ) ;
#18476=VECTOR ( 'NONE', #19634, 1000.000000000000000 ) ;
#18477=CARTESIAN_POINT ( 'NONE',  ( -12.18398860626900060, 28.73617430169795739, 5.000000000000000000 ) ) ;
#18478=DIRECTION ( 'NONE',  ( 0.7071067811865487940, 0.7071067811865463515, 0.000000000000000000 ) ) ;
#18482=LINE ( 'NONE', #106947, #48982 ) ;
#18483=ORIENTED_EDGE ( 'NONE', *, *, #77848, .F. ) ;
#18484=AXIS2_PLACEMENT_3D ( 'NONE', #125940, #132006, #32700 ) ;
#18485=EDGE_CURVE ( 'NONE', #59881, #61485, #91415, .T. ) ;
#18486=DIRECTION ( 'NONE',  ( -0.3543493200069162685, -0.000000000000000000, -0.9351131265310288487 ) ) ;
#18487=EDGE_CURVE ( 'NONE', #11133, #77537, #135629, .T. ) ;
#18489=CARTESIAN_POINT ( 'NONE',  ( -41.99451991528749062, 28.92564299267967343, 4.000000000000000000 ) ) ;
#18491=VECTOR ( 'NONE', #130083, 1000.000000000000000 ) ;
#18492=CARTESIAN_POINT ( 'NONE',  ( 0.000000000000000000, 0.000000000000000000, 5.000000000000000000 ) ) ;
#18493=CARTESIAN_POINT ( 'NONE',  ( 3.299744871391591339, -27.71228299555208352, 4.000000000000000000 ) ) ;
#18494=VERTEX_POINT ( 'NONE', #123342 ) ;
#18495=ORIENTED_EDGE ( 'NONE', *, *, #110960, .F. ) ;
#18496=EDGE_LOOP ( 'NONE', ( #21483, #82731, #107887, #88474 ) ) ;
#18497=DIRECTION ( 'NONE',  ( 0.7071067811865487940, 0.7071067811865463515, -0.000000000000000000 ) ) ;
#18498=CARTESIAN_POINT ( 'NONE',  ( -50.99451991528749062, 28.92564299267973738, 4.000000000000000000 ) ) ;
#18499=VECTOR ( 'NONE', #103237, 1000.000000000000000 ) ;
#18500=LINE ( 'NONE', #106959, #97857 ) ;
#18501=FACE_OUTER_BOUND ( 'NONE', #121149, .T. ) ;
#18502=EDGE_CURVE ( 'NONE', #28383, #59940, #59512, .T. ) ;
#18503=CARTESIAN_POINT ( 'NONE',  ( 21.98911971346036154, -22.02621442084248216, 4.990779571109222879 ) ) ;
#18505=LINE ( 'NONE', #85934, #88060 ) ;
#18506=DIRECTION ( 'NONE',  ( 1.000000000000000000, 0.000000000000000000, 0.000000000000000000 ) ) ;
#18507=CARTESIAN_POINT ( 'NONE',  ( 12.32816939922345334, 14.25929247661557753, 4.000000000000000000 ) ) ;
#18508=LINE ( 'NONE', #138188, #86047 ) ;
#18509=ORIENTED_EDGE ( 'NONE', *, *, #139934, .T. ) ;
#18511=EDGE_LOOP ( 'NONE', ( #136556, #58545, #66967, #141346 ) ) ;
#18512=VECTOR ( 'NONE', #115445, 1000.000000000000000 ) ;
#18513=LINE ( 'NONE', #51910, #50135 ) ;
#18514=CARTESIAN_POINT ( 'NONE',  ( -24.48921356237309510, -27.52281430457072631, 5.000000000000000000 ) ) ;
#18515=ORIENTED_EDGE ( 'NONE', *, *, #122013, .T. ) ;
#18516=FACE_OUTER_BOUND ( 'NONE', #54593, .T. ) ;
#18517=LINE ( 'NONE', #114962, #106609 ) ;
#18518=ORIENTED_EDGE ( 'NONE', *, *, #42064, .F. ) ;
#18519=CARTESIAN_POINT ( 'NONE',  ( -1.499999999999989120, -13.53360074219760278, 5.000000000000000000 ) ) ;
#18520=FACE_OUTER_BOUND ( 'NONE', #113894, .T. ) ;
#18521=VERTEX_POINT ( 'NONE', #68267 ) ;
#18522=ORIENTED_EDGE ( 'NONE', *, *, #97338, .T. ) ;
#18523=DIRECTION ( 'NONE',  ( -0.6830127018922180770, -0.6830127018922204085, -0.2588190451025213501 ) ) ;
#18524=DIRECTION ( 'NONE',  ( 0.000000000000000000, 1.000000000000000000, -0.000000000000000000 ) ) ;
#18525=VECTOR ( 'NONE', #108373, 1000.000000000000000 ) ;
#18526=CARTESIAN_POINT ( 'NONE',  ( 9.707106781186473299, -15.74070752338412049, 5.000000000000000000 ) ) ;
#18529=DIRECTION ( 'NONE',  ( -0.6830127018922180770, -0.6830127018922204085, -0.2588190451025213501 ) ) ;
#18530=VERTEX_POINT ( 'NONE', #81263 ) ;
#18531=DIRECTION ( 'NONE',  ( 0.6830127018922181881, 0.6830127018922202975, -0.2588190451025214056 ) ) ;
#18532=ADVANCED_FACE ( 'NONE', ( #103669 ), #36315, .F. ) ;
#18533=CARTESIAN_POINT ( 'NONE',  ( 26.99999999999982592, -16.44781430457065952, 5.000000000000000000 ) ) ;
#18535=DIRECTION ( 'NONE',  ( 0.7071067811865486830, -0.7071067811865464625, -0.000000000000000000 ) ) ;
#18536=ORIENTED_EDGE ( 'NONE', *, *, #35952, .F. ) ;
#18538=ORIENTED_EDGE ( 'NONE', *, *, #95965, .T. ) ;
#18539=VECTOR ( 'NONE', #53456, 999.9999999999998863 ) ;
#18541=LINE ( 'NONE', #9080, #63985 ) ;
#18542=DIRECTION ( 'NONE',  ( 0.7071067811865486830, -0.7071067811865464625, -0.000000000000000000 ) ) ;
#18543=ORIENTED_EDGE ( 'NONE', *, *, #131093, .F. ) ;
#18546=AXIS2_PLACEMENT_3D ( 'NONE', #34214, #112482, #79179 ) ;
#18547=FACE_OUTER_BOUND ( 'NONE', #112725, .T. ) ;
#18548=VECTOR ( 'NONE', #50586, 1000.000000000000000 ) ;
#18549=DIRECTION ( 'NONE',  ( -0.6830127018922181881, 0.6830127018922202975, -0.2588190451025214056 ) ) ;
#18551=EDGE_CURVE ( 'NONE', #132258, #63562, #137047, .T. ) ;
#18552=DIRECTION ( 'NONE',  ( 0.6830127018922181881, 0.6830127018922202975, -0.2588190451025214056 ) ) ;
#18553=ORIENTED_EDGE ( 'NONE', *, *, #26211, .T. ) ;
#18556=DIRECTION ( 'NONE',  ( -0.7071067811865487940, 0.7071067811865463515, -0.000000000000000000 ) ) ;
#18557=CARTESIAN_POINT ( 'NONE',  ( -27.87485380690749182, -14.24070752338412937, 9.401115078912724243 ) ) ;
#18558=AXIS2_PLACEMENT_3D ( 'NONE', #89193, #92026, #24631 ) ;
#18559=DIRECTION ( 'NONE',  ( -0.7071067811865487940, 0.7071067811865463515, -0.000000000000000000 ) ) ;
#18560=EDGE_CURVE ( 'NONE', #20671, #47204, #126177, .T. ) ;
#18561=ORIENTED_EDGE ( 'NONE', *, *, #6803, .F. ) ;
#18562=ORIENTED_EDGE ( 'NONE', *, *, #124531, .F. ) ;
#18565=EDGE_CURVE ( 'NONE', #57582, #95196, #124036, .T. ) ;
#18566=CARTESIAN_POINT ( 'NONE',  ( 21.79289321881331176, -8.240707523384200428, 5.000000000000000000 ) ) ;
#18567=FACE_OUTER_BOUND ( 'NONE', #141903, .T. ) ;
#18568=VECTOR ( 'NONE', #58015, 1000.000000000000000 ) ;
#18569=CARTESIAN_POINT ( 'NONE',  ( -75.29974487139158157, -27.71228299555258445, 4.000000000000000000 ) ) ;
#18570=DIRECTION ( 'NONE',  ( -0.7071067811865487940, 0.7071067811865463515, -0.000000000000000000 ) ) ;
#18572=DIRECTION ( 'NONE',  ( -0.000000000000000000, 0.3543493200069153248, 0.9351131265310292928 ) ) ;
#18573=FACE_OUTER_BOUND ( 'NONE', #91036, .T. ) ;
#18574=EDGE_CURVE ( 'NONE', #79366, #21205, #13805, .T. ) ;
#18575=AXIS2_PLACEMENT_3D ( 'NONE', #1620, #135072, #11796 ) ;
#18576=VERTEX_POINT ( 'NONE', #94945 ) ;
#18578=LINE ( 'NONE', #61451, #14251 ) ;
#18579=AXIS2_PLACEMENT_3D ( 'NONE', #116272, #129271, #16963 ) ;
#18580=CARTESIAN_POINT ( 'NONE',  ( 34.92499999999998295, 19.70193056682078137, 4.500000000000000888 ) ) ;
#18581=LINE ( 'NONE', #62860, #132614 ) ;
#18583=VECTOR ( 'NONE', #22774, 1000.000000000000000 ) ;
#18584=VERTEX_POINT ( 'NONE', #71814 ) ;
#18585=ORIENTED_EDGE ( 'NONE', *, *, #55046, .T. ) ;
#18586=AXIS2_PLACEMENT_3D ( 'NONE', #123019, #4022, #49038 ) ;
#18587=DIRECTION ( 'NONE',  ( -2.781805975412905890E-17, 0.3543493200069152693, 0.9351131265310292928 ) ) ;
#18588=CARTESIAN_POINT ( 'NONE',  ( 6.299744871391586898, -27.71228299555210484, 4.000000000000000000 ) ) ;
#18591=EDGE_CURVE ( 'NONE', #29382, #87099, #40604, .T. ) ;
#18592=EDGE_CURVE ( 'NONE', #129881, #124632, #28294, .T. ) ;
#18596=ORIENTED_EDGE ( 'NONE', *, *, #78062, .T. ) ;
#18597=VECTOR ( 'NONE', #75618, 1000.000000000000000 ) ;
#18598=ORIENTED_EDGE ( 'NONE', *, *, #87740, .F. ) ;
#18599=ORIENTED_EDGE ( 'NONE', *, *, #15752, .F. ) ;
#18603=CARTESIAN_POINT ( 'NONE',  ( -16.11017322888198677, -22.22500000000000142, 4.785647885939350310 ) ) ;
#18604=LINE ( 'NONE', #60017, #135840 ) ;
#18605=EDGE_CURVE ( 'NONE', #9454, #69693, #127606, .T. ) ;
#18606=EDGE_CURVE ( 'NONE', #35602, #123337, #137778, .T. ) ;
#18609=DIRECTION ( 'NONE',  ( -0.000000000000000000, 0.000000000000000000, 1.000000000000000000 ) ) ;
#18610=DIRECTION ( 'NONE',  ( -0.7071067811865486830, 0.7071067811865464625, -0.000000000000000000 ) ) ;
#18611=CARTESIAN_POINT ( 'NONE',  ( 3.707013264293012256, -21.74070752338405654, 4.999753212805217117 ) ) ;
#18613=VECTOR ( 'NONE', #136348, 1000.000000000000000 ) ;
#18614=DIRECTION ( 'NONE',  ( 1.000000000000000000, 0.000000000000000000, 0.000000000000000000 ) ) ;
#18615=VERTEX_POINT ( 'NONE', #138483 ) ;
#18617=LINE ( 'NONE', #10603, #54215 ) ;
#18619=ORIENTED_EDGE ( 'NONE', *, *, #70626, .F. ) ;
#18620=DIRECTION ( 'NONE',  ( 0.3543493200069162685, -0.000000000000000000, -0.9351131265310288487 ) ) ;
#18621=ORIENTED_EDGE ( 'NONE', *, *, #117888, .T. ) ;
#18622=EDGE_CURVE ( 'NONE', #126064, #92829, #50755, .T. ) ;
#18624=ORIENTED_EDGE ( 'NONE', *, *, #126008, .T. ) ;
#18628=ORIENTED_EDGE ( 'NONE', *, *, #83180, .T. ) ;
#18630=DIRECTION ( 'NONE',  ( 0.6830127018922181881, 0.6830127018922202975, -0.2588190451025214056 ) ) ;
#18634=CARTESIAN_POINT ( 'NONE',  ( 5.999999999999960032, -8.731860332648835765, -2.120594902707523932 ) ) ;
#18635=VECTOR ( 'NONE', #71890, 999.9999999999998863 ) ;
#18639=CARTESIAN_POINT ( 'NONE',  ( 28.82816939922332367, -11.24070752338416490, 4.000000000000000000 ) ) ;
#18640=AXIS2_PLACEMENT_3D ( 'NONE', #88379, #79681, #13628 ) ;
#18643=ORIENTED_EDGE ( 'NONE', *, *, #102150, .F. ) ;
#18644=LINE ( 'NONE', #51318, #127032 ) ;
#18646=EDGE_LOOP ( 'NONE', ( #72572, #2021, #8299, #142152 ) ) ;
#18647=ORIENTED_EDGE ( 'NONE', *, *, #111149, .F. ) ;
#18649=VECTOR ( 'NONE', #49410, 999.9999999999998863 ) ;
#18650=VECTOR ( 'NONE', #93254, 1000.000000000000227 ) ;
#18651=ORIENTED_EDGE ( 'NONE', *, *, #3909, .T. ) ;
#18652=VECTOR ( 'NONE', #5488, 999.9999999999998863 ) ;
#18653=VECTOR ( 'NONE', #14324, 1000.000000000000000 ) ;
#18654=( BOUNDED_CURVE ( )  B_SPLINE_CURVE ( 3, ( #134662, #125918, #2672, #114982 ),
 .UNSPECIFIED., .F., .T. ) 
 B_SPLINE_CURVE_WITH_KNOTS ( ( 4, 4 ),
 ( 1.864375635226932282, 1.933014472006533868 ),
 .UNSPECIFIED. ) 
 CURVE ( )  GEOMETRIC_REPRESENTATION_ITEM ( )  RATIONAL_B_SPLINE_CURVE ( ( 1.000000000000000000, 0.9996074310407765395, 0.9996074310407765395, 1.000000000000000000 ) ) 
 REPRESENTATION_ITEM ( '' )  );
#18655=AXIS2_PLACEMENT_3D ( 'NONE', #65793, #122982, #44757 ) ;
#18656=LINE ( 'NONE', #83976, #30734 ) ;
#18657=FACE_OUTER_BOUND ( 'NONE', #70088, .T. ) ;
#18658=CARTESIAN_POINT ( 'NONE',  ( -2.999999999999975131, -16.06887692260765377, 4.000000000000000000 ) ) ;
#18659=ORIENTED_EDGE ( 'NONE', *, *, #91601, .T. ) ;
#18660=CIRCLE ( 'NONE', #25725, 5.968999999999998529 ) ;
#18661=VERTEX_POINT ( 'NONE', #51478 ) ;
#18662=ADVANCED_FACE ( 'NONE', ( #39906 ), #38455, .T. ) ;
#18665=DIRECTION ( 'NONE',  ( -0.6830127018922181881, 0.6830127018922202975, -0.2588190451025214056 ) ) ;
#18666=VECTOR ( 'NONE', #100120, 999.9999999999998863 ) ;
#18668=ORIENTED_EDGE ( 'NONE', *, *, #117666, .T. ) ;
#18669=VERTEX_POINT ( 'NONE', #96357 ) ;
#18670=ORIENTED_EDGE ( 'NONE', *, *, #19483, .F. ) ;
#18672=VECTOR ( 'NONE', #6905, 1000.000000000000227 ) ;
#18673=CARTESIAN_POINT ( 'NONE',  ( 33.18398860626899705, 28.73617430169810305, 5.000000000000000000 ) ) ;
#18674=CARTESIAN_POINT ( 'NONE',  ( 16.17183060077635659, 12.75929247661558641, 4.000000000000000000 ) ) ;
#18675=DIRECTION ( 'NONE',  ( 0.6830127018922180770, 0.6830127018922202975, -0.2588190451025213501 ) ) ;
#18678=FACE_OUTER_BOUND ( 'NONE', #8464, .T. ) ;
#18679=AXIS2_PLACEMENT_3D ( 'NONE', #25211, #123845, #90486 ) ;
#18680=VECTOR ( 'NONE', #94530, 1000.000000000000000 ) ;
#18683=DIRECTION ( 'NONE',  ( -0.7071067811865486830, -0.7071067811865464625, 0.000000000000000000 ) ) ;
#18684=VECTOR ( 'NONE', #31952, 1000.000000000000227 ) ;
#18685=VERTEX_POINT ( 'NONE', #29004 ) ;
#18686=DIRECTION ( 'NONE',  ( -0.6830127018922180770, -0.6830127018922204085, -0.2588190451025213501 ) ) ;
#18687=LINE ( 'NONE', #105691, #77168 ) ;
#18688=AXIS2_PLACEMENT_3D ( 'NONE', #25484, #69762, #14628 ) ;
#18689=ORIENTED_EDGE ( 'NONE', *, *, #29371, .F. ) ;
#18690=CARTESIAN_POINT ( 'NONE',  ( 32.99999999999976552, -5.527737879153157508, -7.983877177622447974 ) ) ;
#18692=VERTEX_POINT ( 'NONE', #18076 ) ;
#18693=VECTOR ( 'NONE', #104649, 1000.000000000000227 ) ;
#18694=FACE_OUTER_BOUND ( 'NONE', #113829, .T. ) ;
#18696=VERTEX_POINT ( 'NONE', #93546 ) ;
#18697=FACE_OUTER_BOUND ( 'NONE', #7817, .T. ) ;
#18701=DIRECTION ( 'NONE',  ( -0.6830127018922180770, -0.6830127018922204085, -0.2588190451025213501 ) ) ;
#18702=VECTOR ( 'NONE', #73481, 1000.000000000000000 ) ;
#18703=DIRECTION ( 'NONE',  ( -0.7071067811865487940, 0.7071067811865463515, -0.000000000000000000 ) ) ;
#18705=LINE ( 'NONE', #39061, #135141 ) ;
#18706=DIRECTION ( 'NONE',  ( -0.7071067811865487940, 0.7071067811865463515, -0.000000000000000000 ) ) ;
#18711=VECTOR ( 'NONE', #104264, 999.9999999999998863 ) ;
#18712=CARTESIAN_POINT ( 'NONE',  ( -26.99999999999981526, -16.60178936734450872, 0.8616154019346856652 ) ) ;
#18716=DIRECTION ( 'NONE',  ( -0.000000000000000000, 0.000000000000000000, 1.000000000000000000 ) ) ;
#18718=ORIENTED_EDGE ( 'NONE', *, *, #103953, .T. ) ;
#18719=EDGE_CURVE ( 'NONE', #111562, #119104, #26849, .T. ) ;
#18721=LINE ( 'NONE', #42671, #10959 ) ;
#18722=EDGE_CURVE ( 'NONE', #116519, #20421, #63086, .T. ) ;
#18723=PLANE ( 'NONE',  #129730 ) ;
#18724=AXIS2_PLACEMENT_3D ( 'NONE', #104067, #1873, #112827 ) ;
#18726=ORIENTED_EDGE ( 'NONE', *, *, #129035, .T. ) ;
#18727=CARTESIAN_POINT ( 'NONE',  ( -14.99999999999989342, -18.03360074219755660, 5.000000000000000000 ) ) ;
#18728=EDGE_CURVE ( 'NONE', #57216, #15048, #71100, .T. ) ;
#18729=CARTESIAN_POINT ( 'NONE',  ( 29.48334561358934991, 22.22500000000000142, 4.500000000000000888 ) ) ;
#18730=LINE ( 'NONE', #63712, #18737 ) ;
#18731=ADVANCED_FACE ( 'NONE', ( #126859 ), #32583, .F. ) ;
#18732=ADVANCED_FACE ( 'NONE', ( #64482 ), #76819, .F. ) ;
#18734=VERTEX_POINT ( 'NONE', #31161 ) ;
#18736=DIRECTION ( 'NONE',  ( 1.000000000000000000, 0.000000000000000000, 0.000000000000000000 ) ) ;
#18737=VECTOR ( 'NONE', #33072, 1000.000000000000000 ) ;
#18738=DIRECTION ( 'NONE',  ( 0.7071067811865487940, 0.7071067811865463515, 0.000000000000000000 ) ) ;
#18739=CARTESIAN_POINT ( 'NONE',  ( 8.510786437626906675, -27.52281430457049183, 5.000000000000000000 ) ) ;
#18740=DIRECTION ( 'NONE',  ( 0.6830127018922181881, 0.6830127018922202975, -0.2588190451025214056 ) ) ;
#18743=ADVANCED_FACE ( 'NONE', ( #31857 ), #86248, .F. ) ;
#18744=ORIENTED_EDGE ( 'NONE', *, *, #86824, .F. ) ;
#18745=ORIENTED_EDGE ( 'NONE', *, *, #118465, .T. ) ;
#18748=EDGE_CURVE ( 'NONE', #6450, #80414, #120243, .T. ) ;
#18751=EDGE_LOOP ( 'NONE', ( #117571, #73751, #79502, #10268 ) ) ;
#18752=AXIS2_PLACEMENT_3D ( 'NONE', #57961, #34048, #124603 ) ;
#18753=DIRECTION ( 'NONE',  ( -0.7071067811865486830, -0.7071067811865464625, -0.000000000000000000 ) ) ;
#18754=LINE ( 'NONE', #95618, #2619 ) ;
#18755=VECTOR ( 'NONE', #43277, 1000.000000000000000 ) ;
#18756=ADVANCED_FACE ( 'NONE', ( #119541 ), #143457, .F. ) ;
#18757=VECTOR ( 'NONE', #78915, 999.9999999999998863 ) ;
#18759=ORIENTED_EDGE ( 'NONE', *, *, #141272, .T. ) ;
#18760=CYLINDRICAL_SURFACE ( 'NONE', #35085, 0.5000000000000004441 ) ;
#18761=VERTEX_POINT ( 'NONE', #129726 ) ;
#18762=CARTESIAN_POINT ( 'NONE',  ( -27.48921356237309155, -27.52281430457074762, 5.000000000000000000 ) ) ;
#18763=VECTOR ( 'NONE', #60091, 1000.000000000000000 ) ;
#18764=VECTOR ( 'NONE', #23545, 1000.000000000000227 ) ;
#18765=DIRECTION ( 'NONE',  ( 0.3543493200069162685, -0.000000000000000000, -0.9351131265310288487 ) ) ;
#18766=VECTOR ( 'NONE', #63849, 1000.000000000000000 ) ;
#18768=PLANE ( 'NONE',  #67023 ) ;
#18769=VECTOR ( 'NONE', #23294, 1000.000000000000000 ) ;
#18770=ORIENTED_EDGE ( 'NONE', *, *, #17301, .T. ) ;
#18772=ORIENTED_EDGE ( 'NONE', *, *, #26796, .F. ) ;
#18773=DIRECTION ( 'NONE',  ( 0.7071067811865486830, -0.7071067811865464625, -0.000000000000000000 ) ) ;
#18774=DIRECTION ( 'NONE',  ( 0.7071067811865487940, 0.7071067811865463515, 0.000000000000000000 ) ) ;
#18776=VECTOR ( 'NONE', #104879, 1000.000000000000000 ) ;
#18777=ADVANCED_FACE ( 'NONE', ( #44174 ), #8618, .F. ) ;
#18779=ORIENTED_EDGE ( 'NONE', *, *, #107356, .T. ) ;
#18780=ORIENTED_EDGE ( 'NONE', *, *, #129605, .T. ) ;
#18781=AXIS2_PLACEMENT_3D ( 'NONE', #105449, #8264, #82311 ) ;
#18783=VERTEX_POINT ( 'NONE', #20238 ) ;
#18784=VERTEX_POINT ( 'NONE', #110806 ) ;
#18785=EDGE_CURVE ( 'NONE', #95585, #101043, #97821, .T. ) ;
#18786=AXIS2_PLACEMENT_3D ( 'NONE', #127768, #111712, #88551 ) ;
#18787=EDGE_CURVE ( 'NONE', #2746, #100224, #109409, .T. ) ;
#18788=VECTOR ( 'NONE', #105073, 1000.000000000000000 ) ;
#18791=ORIENTED_EDGE ( 'NONE', *, *, #129229, .T. ) ;
#18792=CARTESIAN_POINT ( 'NONE',  ( -14.09068777029287567, 6.496774105546209377, 4.000000000000000000 ) ) ;
#18793=EDGE_CURVE ( 'NONE', #62749, #109346, #131165, .T. ) ;
#18794=VECTOR ( 'NONE', #115786, 1000.000000000000000 ) ;
#18795=CARTESIAN_POINT ( 'NONE',  ( -32.20666063542130075, 21.75929247661549226, 4.998822639870715179 ) ) ;
#18796=FACE_OUTER_BOUND ( 'NONE', #96396, .T. ) ;
#18797=VECTOR ( 'NONE', #55668, 1000.000000000000227 ) ;
#18798=DIRECTION ( 'NONE',  ( -0.7071067811865486830, 0.7071067811865464625, 0.000000000000000000 ) ) ;
#18799=ORIENTED_EDGE ( 'NONE', *, *, #29230, .F. ) ;
#18801=LINE ( 'NONE', #63070, #139033 ) ;
#18802=CARTESIAN_POINT ( 'NONE',  ( -8.241399257801971245, 21.72500000000000142, 5.000000000000000000 ) ) ;
#18803=EDGE_LOOP ( 'NONE', ( #72570, #98156, #96062, #7959 ) ) ;
#18804=DIRECTION ( 'NONE',  ( -0.7071067811865487940, 0.7071067811865463515, -0.000000000000000000 ) ) ;
#18806=VECTOR ( 'NONE', #126245, 1000.000000000000000 ) ;
#18807=LINE ( 'NONE', #94934, #26026 ) ;
#18808=ORIENTED_EDGE ( 'NONE', *, *, #48578, .T. ) ;
#18809=CARTESIAN_POINT ( 'NONE',  ( 22.49999999999985434, 19.46639925780206326, 5.000000000000000000 ) ) ;
#18811=VERTEX_POINT ( 'NONE', #87662 ) ;
#18812=EDGE_CURVE ( 'NONE', #129071, #83273, #44926, .T. ) ;
#18813=EDGE_LOOP ( 'NONE', ( #139549, #62137, #113217, #15765 ) ) ;
#18814=DIRECTION ( 'NONE',  ( 0.7071067811865487940, 0.7071067811865463515, 0.000000000000000000 ) ) ;
#18817=DIRECTION ( 'NONE',  ( 0.7071067811865486830, -0.7071067811865464625, -0.000000000000000000 ) ) ;
#18820=ADVANCED_FACE ( 'NONE', ( #10091 ), #20961, .F. ) ;
#18821=CARTESIAN_POINT ( 'NONE',  ( -17.67183060077634593, -6.740707523384212863, 4.000000000000000000 ) ) ;
#18823=DIRECTION ( 'NONE',  ( -0.000000000000000000, -0.3543493200069152693, 0.9351131265310292928 ) ) ;
#18824=VECTOR ( 'NONE', #134636, 1000.000000000000000 ) ;
#18825=DIRECTION ( 'NONE',  ( -0.6830127018922181881, 0.6830127018922202975, -0.2588190451025214056 ) ) ;
#18826=CARTESIAN_POINT ( 'NONE',  ( -17.51078643762690845, -27.52281430457043143, 5.000000000000000000 ) ) ;
#18827=CARTESIAN_POINT ( 'NONE',  ( -25.17183060077629619, -5.240707523384230626, 4.000000000000000000 ) ) ;
#18828=CARTESIAN_POINT ( 'NONE',  ( 15.18398860626900237, 28.73617430169797871, 5.000000000000000000 ) ) ;
#18830=VERTEX_POINT ( 'NONE', #43448 ) ;
#18831=ORIENTED_EDGE ( 'NONE', *, *, #109264, .T. ) ;
#18835=VERTEX_POINT ( 'NONE', #141320 ) ;
#18836=VERTEX_POINT ( 'NONE', #77531 ) ;
#18837=CARTESIAN_POINT ( 'NONE',  ( -29.99999999999978328, -1.447814304570818500, 5.000000000000000000 ) ) ;
#18840=LINE ( 'NONE', #129753, #9210 ) ;
#18841=EDGE_CURVE ( 'NONE', #75908, #106956, #118856, .T. ) ;
#18842=ORIENTED_EDGE ( 'NONE', *, *, #112077, .T. ) ;
#18843=LINE ( 'NONE', #63112, #2365 ) ;
#18844=VECTOR ( 'NONE', #71173, 1000.000000000000227 ) ;
#18845=ORIENTED_EDGE ( 'NONE', *, *, #26958, .T. ) ;
#18847=CARTESIAN_POINT ( 'NONE',  ( 28.93003974513574050, -0.7407075233842770334, 13.87443053587604069 ) ) ;
#18848=DIRECTION ( 'NONE',  ( -0.000000000000000000, -0.3543493200069152693, 0.9351131265310292928 ) ) ;
#18850=ORIENTED_EDGE ( 'NONE', *, *, #94042, .F. ) ;
#18852=CARTESIAN_POINT ( 'NONE',  ( -13.49999999999989697, 0.05218569542916363935, 5.000000000000000000 ) ) ;
#18855=ORIENTED_EDGE ( 'NONE', *, *, #57855, .T. ) ;
#18856=ORIENTED_EDGE ( 'NONE', *, *, #109458, .F. ) ;
#18857=FACE_OUTER_BOUND ( 'NONE', #45005, .T. ) ;
#18858=VERTEX_POINT ( 'NONE', #56516 ) ;
#18859=DIRECTION ( 'NONE',  ( 0.7071067811865487940, -0.7071067811865463515, 0.000000000000000000 ) ) ;
#18860=DIRECTION ( 'NONE',  ( -0.7071067811865486830, 0.7071067811865464625, 0.000000000000000000 ) ) ;
#18862=DIRECTION ( 'NONE',  ( 0.7071067811865487940, 0.7071067811865463515, 0.000000000000000000 ) ) ;
#18863=CARTESIAN_POINT ( 'NONE',  ( 0.000000000000000000, 0.000000000000000000, 5.000000000000000000 ) ) ;
#18864=ORIENTED_EDGE ( 'NONE', *, *, #108336, .T. ) ;
#18865=ADVANCED_FACE ( 'NONE', ( #134034 ), #34011, .F. ) ;
#18866=AXIS2_PLACEMENT_3D ( 'NONE', #88025, #11862, #55408 ) ;
#18867=CARTESIAN_POINT ( 'NONE',  ( 27.18398860626900060, 28.73617430169806042, 5.000000000000000000 ) ) ;
#18868=VECTOR ( 'NONE', #93158, 999.9999999999998863 ) ;
#18871=DIRECTION ( 'NONE',  ( -0.000000000000000000, 0.3543493200069153248, 0.9351131265310292928 ) ) ;
#18872=ORIENTED_EDGE ( 'NONE', *, *, #100107, .F. ) ;
#18873=CARTESIAN_POINT ( 'NONE',  ( 8.700255128608413102, -27.71228299555199825, 4.000000000000000000 ) ) ;
#18874=VECTOR ( 'NONE', #140325, 999.9999999999998863 ) ;
#18876=AXIS2_PLACEMENT_3D ( 'NONE', #43506, #76885, #121054 ) ;
#18879=VECTOR ( 'NONE', #73271, 1000.000000000000000 ) ;
#18880=VERTEX_POINT ( 'NONE', #78959 ) ;
#18883=ORIENTED_EDGE ( 'NONE', *, *, #17903, .T. ) ;
#18884=EDGE_CURVE ( 'NONE', #27936, #115169, #14383, .T. ) ;
#18885=DIRECTION ( 'NONE',  ( -0.7071067811865487940, 0.7071067811865463515, 0.000000000000000000 ) ) ;
#18886=VECTOR ( 'NONE', #56803, 1000.000000000000000 ) ;
#18887=CARTESIAN_POINT ( 'NONE',  ( -30.29974487139158867, -27.71228299555227537, 4.000000000000000000 ) ) ;
#18889=CARTESIAN_POINT ( 'NONE',  ( -34.92500000000001137, 22.22500000000000142, 4.000000000000000000 ) ) ;
#18890=LINE ( 'NONE', #10154, #12776 ) ;
#18892=VECTOR ( 'NONE', #88742, 999.9999999999998863 ) ;
#18893=DIRECTION ( 'NONE',  ( -0.3543493200069162685, -0.000000000000000000, -0.9351131265310288487 ) ) ;
#18895=FACE_OUTER_BOUND ( 'NONE', #108155, .T. ) ;
#18896=CARTESIAN_POINT ( 'NONE',  ( 9.299744871391588674, -27.71228299555212971, 4.000000000000000000 ) ) ;
#18897=PLANE ( 'NONE',  #76680 ) ;
#18898=CARTESIAN_POINT ( 'NONE',  ( 19.49999999999986855, 12.05218569542904206, 5.000000000000000000 ) ) ;
#18899=LINE ( 'NONE', #52248, #72206 ) ;
#18900=LINE ( 'NONE', #92894, #48318 ) ;
#18901=CARTESIAN_POINT ( 'NONE',  ( 36.18398860626899705, 28.73617430169812437, 5.000000000000000000 ) ) ;
#18902=PLANE ( 'NONE',  #107890 ) ;
#18903=EDGE_LOOP ( 'NONE', ( #75529, #101583, #32914 ) ) ;
#18904=VECTOR ( 'NONE', #110249, 999.9999999999998863 ) ;
#18905=ORIENTED_EDGE ( 'NONE', *, *, #115834, .F. ) ;
#18906=ORIENTED_EDGE ( 'NONE', *, *, #19200, .T. ) ;
#18908=VECTOR ( 'NONE', #83738, 1000.000000000000227 ) ;
#18909=ORIENTED_EDGE ( 'NONE', *, *, #48732, .T. ) ;
#18910=ORIENTED_EDGE ( 'NONE', *, *, #64111, .F. ) ;
#18912=AXIS2_PLACEMENT_3D ( 'NONE', #15417, #127811, #116202 ) ;
#18913=ORIENTED_EDGE ( 'NONE', *, *, #12121, .T. ) ;
#18914=DIRECTION ( 'NONE',  ( 0.7071067811865486830, -0.7071067811865464625, -0.000000000000000000 ) ) ;
#18916=AXIS2_PLACEMENT_3D ( 'NONE', #81373, #59620, #103776 ) ;
#18917=ORIENTED_EDGE ( 'NONE', *, *, #82014, .F. ) ;
#18918=FACE_OUTER_BOUND ( 'NONE', #21196, .T. ) ;
#18919=FACE_OUTER_BOUND ( 'NONE', #82715, .T. ) ;
#18920=PLANE ( 'NONE',  #50995 ) ;
#18923=ORIENTED_EDGE ( 'NONE', *, *, #97764, .T. ) ;
#18924=ADVANCED_FACE ( 'NONE', ( #2781 ), #79699, .F. ) ;
#18927=CARTESIAN_POINT ( 'NONE',  ( -24.71230993966011269, -21.73547319004781286, 4.999917730833664642 ) ) ;
#18928=DIRECTION ( 'NONE',  ( -0.7071067811865486830, -0.7071067811865464625, 0.000000000000000000 ) ) ;
#18929=VECTOR ( 'NONE', #31492, 1000.000000000000000 ) ;
#18930=FACE_OUTER_BOUND ( 'NONE', #143370, .T. ) ;
#18933=LINE ( 'NONE', #6584, #67706 ) ;
#18934=ADVANCED_FACE ( 'NONE', ( #122413 ), #90527, .F. ) ;
#18935=ADVANCED_FACE ( 'NONE', ( #25980 ), #2034, .F. ) ;
#18936=ORIENTED_EDGE ( 'NONE', *, *, #42361, .F. ) ;
#18937=ORIENTED_EDGE ( 'NONE', *, *, #18841, .F. ) ;
#18939=ADVANCED_FACE ( 'NONE', ( #3477 ), #123882, .T. ) ;
#18940=ORIENTED_EDGE ( 'NONE', *, *, #20016, .T. ) ;
#18942=EDGE_CURVE ( 'NONE', #82308, #70075, #112285, .T. ) ;
#18943=VECTOR ( 'NONE', #113082, 1000.000000000000000 ) ;
#18944=DIRECTION ( 'NONE',  ( 0.7071067811865486830, -0.7071067811865464625, -0.000000000000000000 ) ) ;
#18945=VECTOR ( 'NONE', #66873, 1000.000000000000000 ) ;
#18946=ADVANCED_FACE ( 'NONE', ( #23079 ), #24540, .F. ) ;
#18948=DIRECTION ( 'NONE',  ( 0.7071067811865487940, 0.7071067811865463515, 0.000000000000000000 ) ) ;
#18949=CARTESIAN_POINT ( 'NONE',  ( -29.99999999999978328, -0.4125381241607550820, 4.000000000000000000 ) ) ;
#18950=CARTESIAN_POINT ( 'NONE',  ( 50.99451991528749062, 28.92564299267973738, 4.000000000000000000 ) ) ;
#18953=VERTEX_POINT ( 'NONE', #67357 ) ;
#18954=DIRECTION ( 'NONE',  ( 0.7071067811865487940, 0.7071067811865463515, 0.000000000000000000 ) ) ;
#18955=ORIENTED_EDGE ( 'NONE', *, *, #47925, .T. ) ;
#18957=CARTESIAN_POINT ( 'NONE',  ( 11.81601139373100651, 28.73617430169779041, 5.000000000000000000 ) ) ;
#18960=ADVANCED_FACE ( 'NONE', ( #101388 ), #57928, .F. ) ;
#18961=LINE ( 'NONE', #131292, #67256 ) ;
#18962=ORIENTED_EDGE ( 'NONE', *, *, #42342, .T. ) ;
#18964=ORIENTED_EDGE ( 'NONE', *, *, #69220, .T. ) ;
#18965=DIRECTION ( 'NONE',  ( 0.6830127018922181881, 0.6830127018922202975, -0.2588190451025214056 ) ) ;
#18966=CARTESIAN_POINT ( 'NONE',  ( -5.485869665262789852, 22.22500000000000142, -6.155586976313258241 ) ) ;
#18967=CARTESIAN_POINT ( 'NONE',  ( 51.29974487139158867, -27.71228299555242103, 4.000000000000000000 ) ) ;
#18968=DIRECTION ( 'NONE',  ( -0.6830127018922181881, 0.6830127018922202975, -0.2588190451025214056 ) ) ;
#18970=EDGE_CURVE ( 'NONE', #33459, #124649, #102121, .T. ) ;
#18972=ORIENTED_EDGE ( 'NONE', *, *, #6168, .T. ) ;
#18975=ORIENTED_EDGE ( 'NONE', *, *, #27618, .T. ) ;
#18979=VECTOR ( 'NONE', #130640, 1000.000000000000227 ) ;
#18980=CARTESIAN_POINT ( 'NONE',  ( -34.47516574401892342, 1.490517612115595636, 4.998110765256835286 ) ) ;
#18983=CARTESIAN_POINT ( 'NONE',  ( 17.61782366839360847, 8.969638207445433054, 4.000000000000000000 ) ) ;
#18984=ADVANCED_FACE ( 'NONE', ( #114404 ), #136158, .F. ) ;
#18985=VECTOR ( 'NONE', #12678, 1000.000000000000000 ) ;
#18986=AXIS2_PLACEMENT_3D ( 'NONE', #112702, #99672, #111256 ) ;
#18988=CARTESIAN_POINT ( 'NONE',  ( -34.92500000000001137, -22.22500000000000142, 4.000000000000000000 ) ) ;
#18990=FACE_BOUND ( 'NONE', #137366, .T. ) ;
#18991=ORIENTED_EDGE ( 'NONE', *, *, #43045, .T. ) ;
#18992=CARTESIAN_POINT ( 'NONE',  ( -57.18398860626899705, 28.73617430169827358, 5.000000000000000000 ) ) ;
#18993=LINE ( 'NONE', #131325, #100023 ) ;
#18994=LINE ( 'NONE', #54503, #122701 ) ;
#18995=ORIENTED_EDGE ( 'NONE', *, *, #74960, .T. ) ;
#18996=LINE ( 'NONE', #141496, #140701 ) ;
#18997=ORIENTED_EDGE ( 'NONE', *, *, #55818, .F. ) ;
#18998=ORIENTED_EDGE ( 'NONE', *, *, #34836, .T. ) ;
#18999=DIRECTION ( 'NONE',  ( -0.7071067811865487940, 0.7071067811865463515, 0.000000000000000000 ) ) ;
#19001=EDGE_LOOP ( 'NONE', ( #98953, #142794, #14574, #41431 ) ) ;
#19003=ORIENTED_EDGE ( 'NONE', *, *, #82912, .T. ) ;
#19004=CARTESIAN_POINT ( 'NONE',  ( 23.67183060077630685, -0.7407075233842701500, 4.000000000000000000 ) ) ;
#19006=ADVANCED_FACE ( 'NONE', ( #28837 ), #126692, .T. ) ;
#19007=ORIENTED_EDGE ( 'NONE', *, *, #122434, .F. ) ;
#19008=CARTESIAN_POINT ( 'NONE',  ( -17.51078643762690845, -27.52281430457043143, 5.000000000000000000 ) ) ;
#19010=VECTOR ( 'NONE', #99362, 1000.000000000000000 ) ;
#19011=CARTESIAN_POINT ( 'NONE',  ( -21.48921356237309155, -27.52281430457070499, 5.000000000000000000 ) ) ;
#19013=DIRECTION ( 'NONE',  ( -0.7071067811865487940, 0.7071067811865463515, 0.000000000000000000 ) ) ;
#19014=DIRECTION ( 'NONE',  ( 0.7071067811865486830, -0.7071067811865464625, -0.000000000000000000 ) ) ;
#19015=VECTOR ( 'NONE', #68121, 999.9999999999998863 ) ;
#19016=FACE_OUTER_BOUND ( 'NONE', #103556, .T. ) ;
#19017=CARTESIAN_POINT ( 'NONE',  ( -15.29974487139158867, -27.71228299555216879, 4.000000000000000000 ) ) ;
#19018=EDGE_LOOP ( 'NONE', ( #89313, #117492, #113179, #28628 ) ) ;
#19019=ORIENTED_EDGE ( 'NONE', *, *, #120542, .F. ) ;
#19020=AXIS2_PLACEMENT_3D ( 'NONE', #108762, #41398, #119645 ) ;
#19021=LINE ( 'NONE', #112460, #75116 ) ;
#19022=CARTESIAN_POINT ( 'NONE',  ( -3.183988606268992161, 28.73617430169789699, 5.000000000000000000 ) ) ;
#19023=ORIENTED_EDGE ( 'NONE', *, *, #26465, .T. ) ;
#19026=CARTESIAN_POINT ( 'NONE',  ( 4.889826771117856019, -22.22500000000000142, 4.785647885939352086 ) ) ;
#19028=CARTESIAN_POINT ( 'NONE',  ( -30.48921356237309510, -27.52281430457076894, 5.000000000000000000 ) ) ;
#19029=VERTEX_POINT ( 'NONE', #48439 ) ;
#19030=DIRECTION ( 'NONE',  ( 0.7071067811865487940, 0.7071067811865463515, 0.000000000000000000 ) ) ;
#19031=FACE_OUTER_BOUND ( 'NONE', #29277, .T. ) ;
#19032=ADVANCED_FACE ( 'NONE', ( #95496 ), #6301, .F. ) ;
#19034=CARTESIAN_POINT ( 'NONE',  ( -15.18398860626900237, 28.73617430169797871, 5.000000000000000000 ) ) ;
#19035=ORIENTED_EDGE ( 'NONE', *, *, #70877, .T. ) ;
#19038=VECTOR ( 'NONE', #106124, 1000.000000000000000 ) ;
#19039=DIRECTION ( 'NONE',  ( -0.6830127018922180770, -0.6830127018922204085, -0.2588190451025213501 ) ) ;
#19040=CARTESIAN_POINT ( 'NONE',  ( -25.49999999999982592, 14.14708470758588987, -0.5283514160165968532 ) ) ;
#19041=ORIENTED_EDGE ( 'NONE', *, *, #76749, .T. ) ;
#19042=CARTESIAN_POINT ( 'NONE',  ( -13.49999999999990230, 21.05218569542895679, 5.000000000000000000 ) ) ;
#19043=AXIS2_PLACEMENT_3D ( 'NONE', #115150, #137680, #14455 ) ;
#19044=ORIENTED_EDGE ( 'NONE', *, *, #97157, .T. ) ;
#19045=DIRECTION ( 'NONE',  ( -0.000000000000000000, 0.3543493200069153248, 0.9351131265310292928 ) ) ;
#19047=CARTESIAN_POINT ( 'NONE',  ( 35.35681257248241138, -20.24070752338406720, 21.22881796311220981 ) ) ;
#19048=ORIENTED_EDGE ( 'NONE', *, *, #118170, .F. ) ;
#19049=EDGE_CURVE ( 'NONE', #16920, #17718, #71632, .T. ) ;
#19050=ADVANCED_FACE ( 'NONE', ( #50583 ), #92634, .F. ) ;
#19051=CARTESIAN_POINT ( 'NONE',  ( 24.48921356237309510, -27.52281430457072631, 5.000000000000000000 ) ) ;
#19053=CARTESIAN_POINT ( 'NONE',  ( -23.20666063542136470, 21.75929247661548516, 4.998822639870711626 ) ) ;
#19054=VECTOR ( 'NONE', #14603, 1000.000000000000000 ) ;
#19055=ORIENTED_EDGE ( 'NONE', *, *, #48422, .F. ) ;
#19056=CARTESIAN_POINT ( 'NONE',  ( -14.99999999999989164, -11.35517001088073208, -1.126524801160144529 ) ) ;
#19057=CARTESIAN_POINT ( 'NONE',  ( -19.49999999999985079, -20.94781430457061333, 5.000000000000000000 ) ) ;
#19058=DIRECTION ( 'NONE',  ( 0.000000000000000000, -1.000000000000000000, 0.000000000000000000 ) ) ;
#19059=ORIENTED_EDGE ( 'NONE', *, *, #736, .T. ) ;
#19060=ADVANCED_FACE ( 'NONE', ( #138309 ), #115790, .F. ) ;
#19061=ORIENTED_EDGE ( 'NONE', *, *, #104505, .F. ) ;
#19062=VECTOR ( 'NONE', #31257, 1000.000000000000000 ) ;
#19063=CARTESIAN_POINT ( 'NONE',  ( -24.48921356237309510, -27.52281430457072631, 5.000000000000000000 ) ) ;
#19064=LINE ( 'NONE', #63326, #20449 ) ;
#19066=PLANE ( 'NONE',  #78345 ) ;
#19067=CARTESIAN_POINT ( 'NONE',  ( 35.99451991528749772, 28.92564299267963079, 4.000000000000000000 ) ) ;
#19068=CARTESIAN_POINT ( 'NONE',  ( 2.671830600776451181, -0.7407075233842770334, 4.000000000000000000 ) ) ;
#19069=VERTEX_POINT ( 'NONE', #137603 ) ;
#19070=CARTESIAN_POINT ( 'NONE',  ( 57.18398860626899705, 28.73617430169827358, 5.000000000000000000 ) ) ;
#19071=CARTESIAN_POINT ( 'NONE',  ( 1.040834085586084257E-14, 14.58746187583908771, 4.000000000000000000 ) ) ;
#19072=CARTESIAN_POINT ( 'NONE',  ( 31.49999999999978684, 7.466399257802189382, 5.000000000000000000 ) ) ;
#19073=VECTOR ( 'NONE', #52069, 1000.000000000000000 ) ;
#19074=VECTOR ( 'NONE', #18478, 999.9999999999998863 ) ;
#19075=VECTOR ( 'NONE', #30381, 999.9999999999998863 ) ;
#19076=PLANE ( 'NONE',  #64487 ) ;
#19078=CARTESIAN_POINT ( 'NONE',  ( -26.99451991528749417, 28.92564299267956685, 4.000000000000000000 ) ) ;
#19079=VECTOR ( 'NONE', #16911, 999.9999999999998863 ) ;
#19080=VERTEX_POINT ( 'NONE', #126016 ) ;
#19081=DIRECTION ( 'NONE',  ( -0.000000000000000000, 0.000000000000000000, 1.000000000000000000 ) ) ;
#19082=ORIENTED_EDGE ( 'NONE', *, *, #5365, .T. ) ;
#19083=ORIENTED_EDGE ( 'NONE', *, *, #116649, .T. ) ;
#19084=AXIS2_PLACEMENT_3D ( 'NONE', #23388, #35023, #3749 ) ;
#19085=DIRECTION ( 'NONE',  ( 0.7071067811865487940, 0.7071067811865463515, 0.000000000000000000 ) ) ;
#19086=MECHANICAL_DESIGN_GEOMETRIC_PRESENTATION_REPRESENTATION('',(#74686),#30704);
#19087=PLANE ( 'NONE',  #48618 ) ;
#19088=ORIENTED_EDGE ( 'NONE', *, *, #59925, .T. ) ;
#19089=CARTESIAN_POINT ( 'NONE',  ( -34.80981832425529632, -18.74070752338408852, 7.910009926591588858 ) ) ;
#19090=EDGE_CURVE ( 'NONE', #131612, #54251, #26686, .T. ) ;
#19091=CARTESIAN_POINT ( 'NONE',  ( -1.954842266633324943, -21.74070752338406010, 21.72585301388583900 ) ) ;
#19092=CARTESIAN_POINT ( 'NONE',  ( -54.29974487139159578, -27.71228299555243879, 4.000000000000000000 ) ) ;
#19093=PLANE ( 'NONE',  #68596 ) ;
#19094=ORIENTED_EDGE ( 'NONE', *, *, #81999, .T. ) ;
#19095=FACE_OUTER_BOUND ( 'NONE', #67625, .T. ) ;
#19097=CARTESIAN_POINT ( 'NONE',  ( 34.82816939922328459, 6.759292476615649470, 4.000000000000000000 ) ) ;
#19098=DIRECTION ( 'NONE',  ( 1.000000000000000000, 0.000000000000000000, 0.000000000000000000 ) ) ;
#19099=LINE ( 'NONE', #116979, #42723 ) ;
#19102=EDGE_CURVE ( 'NONE', #16920, #89076, #84642, .T. ) ;
#19103=VECTOR ( 'NONE', #103880, 1000.000000000000000 ) ;
#19104=DIRECTION ( 'NONE',  ( 0.6830127018922180770, -0.6830127018922204085, -0.2588190451025213501 ) ) ;
#19106=ORIENTED_EDGE ( 'NONE', *, *, #120231, .F. ) ;
#19109=EDGE_CURVE ( 'NONE', #35471, #14309, #16498, .T. ) ;
#19110=DIRECTION ( 'NONE',  ( -8.817971600062199903E-18, 0.3543493200069153248, 0.9351131265310292928 ) ) ;
#19111=ADVANCED_FACE ( 'NONE', ( #37579 ), #51308, .F. ) ;
#19112=PLANE ( 'NONE',  #32171 ) ;
#19113=ORIENTED_EDGE ( 'NONE', *, *, #92054, .T. ) ;
#19114=EDGE_CURVE ( 'NONE', #89949, #33791, #5619, .T. ) ;
#19115=VECTOR ( 'NONE', #87311, 1000.000000000000000 ) ;
#19116=CARTESIAN_POINT ( 'NONE',  ( 31.49999999999977973, 3.653845994658420970, -4.504631822206443204 ) ) ;
#19118=AXIS2_PLACEMENT_3D ( 'NONE', #81665, #126544, #47618 ) ;
#19119=ORIENTED_EDGE ( 'NONE', *, *, #38630, .F. ) ;
#19125=LINE ( 'NONE', #72126, #583 ) ;
#19126=CARTESIAN_POINT ( 'NONE',  ( 47.99451991528749062, 28.92564299267971251, 4.000000000000000000 ) ) ;
#19127=CARTESIAN_POINT ( 'NONE',  ( -45.18398860626900415, 28.73617430169818832, 5.000000000000000000 ) ) ;
#19128=EDGE_CURVE ( 'NONE', #22127, #137445, #73079, .T. ) ;
#19129=EDGE_LOOP ( 'NONE', ( #100706, #36273, #44236, #72377 ) ) ;
#19130=EDGE_CURVE ( 'NONE', #56540, #4701, #139026, .T. ) ;
#19131=DIRECTION ( 'NONE',  ( 0.7071067811865486830, -0.7071067811865464625, -0.000000000000000000 ) ) ;
#19132=DIRECTION ( 'NONE',  ( -0.000000000000000000, 0.3543493200069153248, 0.9351131265310292928 ) ) ;
#19134=LINE ( 'NONE', #120551, #87845 ) ;
#19135=CARTESIAN_POINT ( 'NONE',  ( -0.8382938754737979670, -6.740707523384212863, 16.75550250614867309 ) ) ;
#19136=CARTESIAN_POINT ( 'NONE',  ( 19.49999999999987210, -10.91253812416064228, 4.000000000000000000 ) ) ;
#19137=CARTESIAN_POINT ( 'NONE',  ( -10.49999999999991651, -14.94781430457067195, 5.000000000000000000 ) ) ;
#19138=EDGE_CURVE ( 'NONE', #131955, #114421, #128161, .T. ) ;
#19139=VERTEX_POINT ( 'NONE', #128845 ) ;
#19140=ORIENTED_EDGE ( 'NONE', *, *, #7099, .F. ) ;
#19142=DIRECTION ( 'NONE',  ( 0.7071067811865486830, -0.7071067811865463515, 0.000000000000000000 ) ) ;
#19144=DIRECTION ( 'NONE',  ( -0.6830127018922181881, 0.6830127018922202975, -0.2588190451025214056 ) ) ;
#19145=VECTOR ( 'NONE', #93877, 1000.000000000000114 ) ;
#19146=CARTESIAN_POINT ( 'NONE',  ( -27.98911971346032601, -22.02621442084248216, 4.990779571109220214 ) ) ;
#19147=CARTESIAN_POINT ( 'NONE',  ( 4.499999999999970690, 6.431123077392120635, 4.000000000000000000 ) ) ;
#19148=ORIENTED_EDGE ( 'NONE', *, *, #4059, .F. ) ;
#19149=ORIENTED_EDGE ( 'NONE', *, *, #127993, .T. ) ;
#19150=EDGE_CURVE ( 'NONE', #27298, #23510, #49177, .T. ) ;
#19151=VECTOR ( 'NONE', #14278, 1000.000000000000000 ) ;
#19152=CARTESIAN_POINT ( 'NONE',  ( 42.18398860626899705, 28.73617430169816700, 5.000000000000000000 ) ) ;
#19153=CARTESIAN_POINT ( 'NONE',  ( 27.29974487139158512, -27.71228299555225405, 4.000000000000000000 ) ) ;
#19155=ORIENTED_EDGE ( 'NONE', *, *, #84240, .T. ) ;
#19156=DIRECTION ( 'NONE',  ( 0.6830127018922181881, 0.6830127018922202975, -0.2588190451025214056 ) ) ;
#19157=ORIENTED_EDGE ( 'NONE', *, *, #107223, .F. ) ;
#19160=EDGE_CURVE ( 'NONE', #64078, #26808, #88218, .T. ) ;
#19161=VECTOR ( 'NONE', #36791, 1000.000000000000227 ) ;
#19162=DIRECTION ( 'NONE',  ( -0.7071067811865486830, -0.7071067811865464625, 0.000000000000000000 ) ) ;
#19163=FACE_BOUND ( 'NONE', #50569, .T. ) ;
#19166=CARTESIAN_POINT ( 'NONE',  ( -78.18398860626899705, 28.73617430169841924, 5.000000000000000000 ) ) ;
#19167=AXIS2_PLACEMENT_3D ( 'NONE', #59285, #103439, #91861 ) ;
#19168=CARTESIAN_POINT ( 'NONE',  ( 7.171830600776422315, -11.24070752338416845, 4.000000000000000000 ) ) ;
#19169=LINE ( 'NONE', #44531, #96780 ) ;
#19170=EDGE_LOOP ( 'NONE', ( #118011, #119347, #142983, #46148 ) ) ;
#19171=CARTESIAN_POINT ( 'NONE',  ( -60.48921356237309510, -27.52281430457097500, 5.000000000000000000 ) ) ;
#19173=ORIENTED_EDGE ( 'NONE', *, *, #31991, .F. ) ;
#19176=ORIENTED_EDGE ( 'NONE', *, *, #54945, .T. ) ;
#19177=CARTESIAN_POINT ( 'NONE',  ( -51.18398860626899705, 28.73617430169823095, 5.000000000000000000 ) ) ;
#19178=DIRECTION ( 'NONE',  ( 0.7071067811865487940, -0.7071067811865463515, 0.000000000000000000 ) ) ;
#19179=EDGE_CURVE ( 'NONE', #140087, #41095, #22209, .T. ) ;
#19180=LINE ( 'NONE', #51111, #5020 ) ;
#19182=VECTOR ( 'NONE', #137093, 1000.000000000000000 ) ;
#19183=CARTESIAN_POINT ( 'NONE',  ( -19.05000000000000071, 3.174999999999997158, 4.000000000000000000 ) ) ;
#19184=CARTESIAN_POINT ( 'NONE',  ( -18.18398860626898994, 28.73617430169800002, 5.000000000000000000 ) ) ;
#19185=FACE_OUTER_BOUND ( 'NONE', #30615, .T. ) ;
#19186=EDGE_CURVE ( 'NONE', #55371, #92458, #29392, .T. ) ;
#19187=DIRECTION ( 'NONE',  ( 0.7071067811865486830, -0.7071067811865464625, -0.000000000000000000 ) ) ;
#19188=LINE ( 'NONE', #64846, #88921 ) ;
#19189=CARTESIAN_POINT ( 'NONE',  ( -14.99999999999990230, -22.22500000000000142, 4.412002311790018894 ) ) ;
#19190=DIRECTION ( 'NONE',  ( -0.6830127018922180770, -0.6830127018922204085, -0.2588190451025213501 ) ) ;
#19192=VECTOR ( 'NONE', #67001, 999.9999999999998863 ) ;
#19194=CARTESIAN_POINT ( 'NONE',  ( -38.99451991528749062, 28.92564299267965211, 4.000000000000000000 ) ) ;
#19197=FACE_OUTER_BOUND ( 'NONE', #33097, .T. ) ;
#19198=VERTEX_POINT ( 'NONE', #87497 ) ;
#19199=VERTEX_POINT ( 'NONE', #19377 ) ;
#19200=EDGE_CURVE ( 'NONE', #14243, #20682, #8453, .T. ) ;
#19201=EDGE_LOOP ( 'NONE', ( #82844, #134131, #29178, #81857 ) ) ;
#19203=ORIENTED_EDGE ( 'NONE', *, *, #96338, .F. ) ;
#19204=FACE_OUTER_BOUND ( 'NONE', #122374, .T. ) ;
#19208=EDGE_LOOP ( 'NONE', ( #89462, #57798, #59589, #138131 ) ) ;
#19209=FACE_OUTER_BOUND ( 'NONE', #67168, .T. ) ;
#19210=ORIENTED_EDGE ( 'NONE', *, *, #85208, .T. ) ;
#19211=DIRECTION ( 'NONE',  ( 0.3543493200069162685, -0.000000000000000000, -0.9351131265310288487 ) ) ;
#19212=DIRECTION ( 'NONE',  ( -0.6830127018922181881, 0.6830127018922202975, -0.2588190451025214056 ) ) ;
#19213=PLANE ( 'NONE',  #125817 ) ;
#19214=VERTEX_POINT ( 'NONE', #129553 ) ;
#19215=ORIENTED_EDGE ( 'NONE', *, *, #134026, .F. ) ;
#19216=DIRECTION ( 'NONE',  ( -0.6830127018922180770, -0.6830127018922204085, -0.2588190451025213501 ) ) ;
#19217=VECTOR ( 'NONE', #56349, 1000.000000000000000 ) ;
#19218=EDGE_CURVE ( 'NONE', #73986, #102653, #93339, .T. ) ;
#19219=DIRECTION ( 'NONE',  ( 0.7071067811865487940, -0.7071067811865463515, 0.000000000000000000 ) ) ;
#19220=VERTEX_POINT ( 'NONE', #141899 ) ;
#19222=ORIENTED_EDGE ( 'NONE', *, *, #43191, .F. ) ;
#19224=EDGE_CURVE ( 'NONE', #120628, #92397, #33157, .T. ) ;
#19227=EDGE_LOOP ( 'NONE', ( #14612, #132302, #134639, #31300 ) ) ;
#19228=FACE_OUTER_BOUND ( 'NONE', #34167, .T. ) ;
#19230=DIRECTION ( 'NONE',  ( 0.7071067811865486830, -0.7071067811865464625, -0.000000000000000000 ) ) ;
#19231=DIRECTION ( 'NONE',  ( 0.7071067811865486830, -0.7071067811865464625, -0.000000000000000000 ) ) ;
#19232=EDGE_CURVE ( 'NONE', #89674, #129739, #75905, .T. ) ;
#19234=ORIENTED_EDGE ( 'NONE', *, *, #114902, .F. ) ;
#19235=EDGE_CURVE ( 'NONE', #140787, #135668, #58252, .T. ) ;
#19236=CARTESIAN_POINT ( 'NONE',  ( 16.96659967656967893, 6.759292476615653023, 12.28218704918526072 ) ) ;
#19237=ORIENTED_EDGE ( 'NONE', *, *, #38013, .T. ) ;
#19238=CARTESIAN_POINT ( 'NONE',  ( -5.999999999999960032, 5.966399257802207146, 5.000000000000000000 ) ) ;
#19240=VECTOR ( 'NONE', #35868, 1000.000000000000114 ) ;
#19241=ORIENTED_EDGE ( 'NONE', *, *, #134164, .T. ) ;
#19243=( BOUNDED_CURVE ( )  B_SPLINE_CURVE ( 3, ( #114751, #14753, #103183, #26354 ),
 .UNSPECIFIED., .F., .T. ) 
 B_SPLINE_CURVE_WITH_KNOTS ( ( 4, 4 ),
 ( 5.920967161967926273, 7.341195215986584977 ),
 .UNSPECIFIED. ) 
 CURVE ( )  GEOMETRIC_REPRESENTATION_ITEM ( )  RATIONAL_B_SPLINE_CURVE ( ( 1.000000000000000000, 0.8388583629366725969, 0.8388583629366725969, 1.000000000000000000 ) ) 
 REPRESENTATION_ITEM ( '' )  );
#19244=LINE ( 'NONE', #9783, #127758 ) ;
#19245=ORIENTED_EDGE ( 'NONE', *, *, #104548, .T. ) ;
#19246=ORIENTED_EDGE ( 'NONE', *, *, #80131, .T. ) ;
#19247=AXIS2_PLACEMENT_3D ( 'NONE', #111914, #12575, #56856 ) ;
#19248=CARTESIAN_POINT ( 'NONE',  ( -11.99999999999990585, -13.44781430457068794, 5.000000000000000000 ) ) ;
#19250=CARTESIAN_POINT ( 'NONE',  ( -25.17183060077629619, -8.240707523384200428, 4.000000000000000000 ) ) ;
#19251=VECTOR ( 'NONE', #136976, 1000.000000000000227 ) ;
#19255=EDGE_CURVE ( 'NONE', #23291, #43567, #43997, .T. ) ;
#19256=DIRECTION ( 'NONE',  ( -0.000000000000000000, 0.000000000000000000, 1.000000000000000000 ) ) ;
#19257=DIRECTION ( 'NONE',  ( 0.7071067811865487940, 0.7071067811865463515, 0.000000000000000000 ) ) ;
#19260=VERTEX_POINT ( 'NONE', #54190 ) ;
#19261=CARTESIAN_POINT ( 'NONE',  ( -17.92867102513379862, 9.037728232668255757, 5.000000000000000000 ) ) ;
#19263=VECTOR ( 'NONE', #13168, 1000.000000000000000 ) ;
#19264=LINE ( 'NONE', #15126, #693 ) ;
#19265=LINE ( 'NONE', #120698, #137952 ) ;
#19266=ORIENTED_EDGE ( 'NONE', *, *, #75462, .T. ) ;
#19267=DIRECTION ( 'NONE',  ( 0.7071067811865487940, -0.7071067811865463515, 0.000000000000000000 ) ) ;
#19268=LINE ( 'NONE', #76527, #39612 ) ;
#19269=EDGE_LOOP ( 'NONE', ( #96117, #12731, #136659, #57032 ) ) ;
#19270=PLANE ( 'NONE',  #129557 ) ;
#19271=CARTESIAN_POINT ( 'NONE',  ( -42.29974487139158157, -27.71228299555235708, 4.000000000000000000 ) ) ;
#19272=CARTESIAN_POINT ( 'NONE',  ( -37.64175702458837236, 15.75929247661555088, 19.34181609438708449 ) ) ;
#19273=ORIENTED_EDGE ( 'NONE', *, *, #42598, .F. ) ;
#19274=AXIS2_PLACEMENT_3D ( 'NONE', #92390, #93133, #27150 ) ;
#19276=CARTESIAN_POINT ( 'NONE',  ( -34.92500000000001137, 22.22500000000000142, 4.000000000000000000 ) ) ;
#19278=CARTESIAN_POINT ( 'NONE',  ( -12.13499573751615124, 3.759292476615685441, 15.36553568819729065 ) ) ;
#19280=DIRECTION ( 'NONE',  ( 0.6830127018922181881, 0.6830127018922202975, -0.2588190451025214056 ) ) ;
#19281=EDGE_CURVE ( 'NONE', #114028, #128067, #131009, .T. ) ;
#19282=CARTESIAN_POINT ( 'NONE',  ( -25.49999999999982236, -5.568876922607755908, 4.000000000000000000 ) ) ;
#19283=ORIENTED_EDGE ( 'NONE', *, *, #28617, .F. ) ;
#19284=LINE ( 'NONE', #75124, #77027 ) ;
#19285=ADVANCED_FACE ( 'NONE', ( #30248 ), #85329, .F. ) ;
#19286=DIRECTION ( 'NONE',  ( -0.000000000000000000, 0.000000000000000000, 1.000000000000000000 ) ) ;
#19288=ORIENTED_EDGE ( 'NONE', *, *, #64644, .F. ) ;
#19289=EDGE_CURVE ( 'NONE', #120806, #14374, #141142, .T. ) ;
#19291=VECTOR ( 'NONE', #7215, 1000.000000000000000 ) ;
#19292=CARTESIAN_POINT ( 'NONE',  ( 41.99451991528749062, 28.92564299267967343, 4.000000000000000000 ) ) ;
#19296=VECTOR ( 'NONE', #86384, 1000.000000000000000 ) ;
#19297=CARTESIAN_POINT ( 'NONE',  ( 42.48921356237308800, -27.52281430457085065, 5.000000000000000000 ) ) ;
#19298=EDGE_LOOP ( 'NONE', ( #83849, #128857, #30648, #94914 ) ) ;
#19299=FACE_OUTER_BOUND ( 'NONE', #30987, .T. ) ;
#19300=DIRECTION ( 'NONE',  ( 0.7071067811865486830, -0.7071067811865464625, -0.000000000000000000 ) ) ;
#19301=EDGE_CURVE ( 'NONE', #114199, #135973, #65790, .T. ) ;
#19303=EDGE_CURVE ( 'NONE', #1414, #97534, #42593, .T. ) ;
#19304=LINE ( 'NONE', #120005, #106429 ) ;
#19306=ORIENTED_EDGE ( 'NONE', *, *, #22569, .F. ) ;
#19307=CARTESIAN_POINT ( 'NONE',  ( 0.1839886062690032631, 28.73617430169787568, 5.000000000000000000 ) ) ;
#19308=LINE ( 'NONE', #63564, #61590 ) ;
#19309=LINE ( 'NONE', #9091, #61027 ) ;
#19311=EDGE_LOOP ( 'NONE', ( #63256, #85091, #4322, #88523 ) ) ;
#19312=EDGE_CURVE ( 'NONE', #102663, #106069, #10617, .T. ) ;
#19313=VERTEX_POINT ( 'NONE', #143295 ) ;
#19316=ORIENTED_EDGE ( 'NONE', *, *, #48524, .T. ) ;
#19317=CARTESIAN_POINT ( 'NONE',  ( -9.183988606268997046, 28.73617430169793607, 5.000000000000000000 ) ) ;
#19318=LINE ( 'NONE', #98321, #57284 ) ;
#19319=CARTESIAN_POINT ( 'NONE',  ( -32.99999999999976552, 10.55218569542905627, 5.000000000000000000 ) ) ;
#19320=LINE ( 'NONE', #10559, #26981 ) ;
#19321=ORIENTED_EDGE ( 'NONE', *, *, #80724, .F. ) ;
#19322=EDGE_CURVE ( 'NONE', #141841, #22237, #102667, .T. ) ;
#19323=CARTESIAN_POINT ( 'NONE',  ( -23.99451991528749062, 28.92564299267954908, 4.000000000000000000 ) ) ;
#19325=VECTOR ( 'NONE', #99789, 1000.000000000000227 ) ;
#19326=EDGE_LOOP ( 'NONE', ( #88045, #35657, #3359, #134927 ) ) ;
#19327=AXIS2_PLACEMENT_3D ( 'NONE', #112418, #137022, #15904 ) ;
#19329=DIRECTION ( 'NONE',  ( 1.000000000000000000, 0.000000000000000000, 0.000000000000000000 ) ) ;
#19330=EDGE_CURVE ( 'NONE', #68806, #106934, #63728, .T. ) ;
#19331=PLANE ( 'NONE',  #130319 ) ;
#19332=ORIENTED_EDGE ( 'NONE', *, *, #47579, .T. ) ;
#19333=VECTOR ( 'NONE', #143147, 1000.000000000000227 ) ;
#19335=FACE_BOUND ( 'NONE', #82899, .T. ) ;
#19337=EDGE_CURVE ( 'NONE', #112685, #81140, #57744, .T. ) ;
#19339=CARTESIAN_POINT ( 'NONE',  ( -36.48921356237310221, -27.52281430457080802, 5.000000000000000000 ) ) ;
#19340=ADVANCED_FACE ( 'NONE', ( #122238 ), #80907, .T. ) ;
#19341=LINE ( 'NONE', #96158, #136042 ) ;
#19342=VECTOR ( 'NONE', #83761, 1000.000000000000114 ) ;
#19343=CARTESIAN_POINT ( 'NONE',  ( 56.99451991528749062, 28.92564299267978001, 4.000000000000000000 ) ) ;
#19345=ADVANCED_FACE ( 'NONE', ( #88944 ), #111365, .F. ) ;
#19346=ORIENTED_EDGE ( 'NONE', *, *, #89352, .F. ) ;
#19347=VECTOR ( 'NONE', #8319, 1000.000000000000000 ) ;
#19349=VERTEX_POINT ( 'NONE', #24372 ) ;
#19350=ORIENTED_EDGE ( 'NONE', *, *, #57228, .F. ) ;
#19352=CARTESIAN_POINT ( 'NONE',  ( -32.99999999999976552, -6.033600742197672950, 5.000000000000000000 ) ) ;
#19353=CARTESIAN_POINT ( 'NONE',  ( -34.49999999999974420, -14.70932175296479549, -11.46312253303829287 ) ) ;
#19354=PLANE ( 'NONE',  #1106 ) ;
#19355=VERTEX_POINT ( 'NONE', #79527 ) ;
#19357=DIRECTION ( 'NONE',  ( -0.7071067811865486830, -0.7071067811865464625, 0.000000000000000000 ) ) ;
#19358=CARTESIAN_POINT ( 'NONE',  ( -20.99999999999985079, -7.068876922607739921, 4.000000000000000000 ) ) ;
#19359=CARTESIAN_POINT ( 'NONE',  ( 1.828169399223516400, 12.75929247661558996, 4.000000000000000000 ) ) ;
#19360=VECTOR ( 'NONE', #106757, 1000.000000000000227 ) ;
#19362=ORIENTED_EDGE ( 'NONE', *, *, #134870, .T. ) ;
#19363=DIRECTION ( 'NONE',  ( 0.7071067811865487940, 0.7071067811865463515, 0.000000000000000000 ) ) ;
#19366=LINE ( 'NONE', #34350, #89783 ) ;
#19367=ORIENTED_EDGE ( 'NONE', *, *, #41600, .T. ) ;
#19371=ORIENTED_EDGE ( 'NONE', *, *, #136334, .F. ) ;
#19372=ORIENTED_EDGE ( 'NONE', *, *, #102377, .T. ) ;
#19374=VECTOR ( 'NONE', #86070, 999.9999999999998863 ) ;
#19377=CARTESIAN_POINT ( 'NONE',  ( -11.67183060077638501, -21.74070752338405654, 4.000000000000000000 ) ) ;
#19378=EDGE_CURVE ( 'NONE', #107763, #57164, #34543, .T. ) ;
#19379=LINE ( 'NONE', #83960, #35125 ) ;
#19381=FACE_OUTER_BOUND ( 'NONE', #46541, .T. ) ;
#19382=VECTOR ( 'NONE', #70225, 1000.000000000000000 ) ;
#19385=ORIENTED_EDGE ( 'NONE', *, *, #96005, .F. ) ;
#19386=CARTESIAN_POINT ( 'NONE',  ( 34.92499999999998295, 1.701930566820966773, 4.500000000000000888 ) ) ;
#19387=EDGE_LOOP ( 'NONE', ( #4705, #40824, #67869, #86844 ) ) ;
#19388=VERTEX_POINT ( 'NONE', #89627 ) ;
#19389=ORIENTED_EDGE ( 'NONE', *, *, #80983, .F. ) ;
#19390=ORIENTED_EDGE ( 'NONE', *, *, #119507, .T. ) ;
#19391=DIRECTION ( 'NONE',  ( 0.7071067811865487940, -0.7071067811865463515, 0.000000000000000000 ) ) ;
#19392=CARTESIAN_POINT ( 'NONE',  ( 34.49999999999976552, -14.94567065516889848, 4.994342998332158778 ) ) ;
#19393=EDGE_CURVE ( 'NONE', #95492, #123094, #25066, .T. ) ;
#19394=DIRECTION ( 'NONE',  ( -0.000000000000000000, -0.3543493200069152693, 0.9351131265310292928 ) ) ;
#19395=ORIENTED_EDGE ( 'NONE', *, *, #128914, .T. ) ;
#19396=EDGE_CURVE ( 'NONE', #51247, #5949, #2596, .T. ) ;
#19398=ORIENTED_EDGE ( 'NONE', *, *, #123556, .T. ) ;
#19399=AXIS2_PLACEMENT_3D ( 'NONE', #104581, #103150, #93713 ) ;
#19402=PLANE ( 'NONE',  #48485 ) ;
#19403=CARTESIAN_POINT ( 'NONE',  ( 9.299744871391588674, -27.71228299555212971, 4.000000000000000000 ) ) ;
#19404=EDGE_CURVE ( 'NONE', #52329, #80109, #1165, .T. ) ;
#19405=DIRECTION ( 'NONE',  ( -0.7071067811865486830, 0.7071067811865464625, 0.000000000000000000 ) ) ;
#19406=VERTEX_POINT ( 'NONE', #80216 ) ;
#19407=ORIENTED_EDGE ( 'NONE', *, *, #52461, .T. ) ;
#19408=ORIENTED_EDGE ( 'NONE', *, *, #12008, .T. ) ;
#19410=CARTESIAN_POINT ( 'NONE',  ( -28.49999999999980460, -1.533600742197721134, 5.000000000000000000 ) ) ;
#19411=CARTESIAN_POINT ( 'NONE',  ( 17.51078643762690845, -27.52281430457043143, 5.000000000000000000 ) ) ;
#19412=CIRCLE ( 'NONE', #63439, 5.968999999999998529 ) ;
#19413=DIRECTION ( 'NONE',  ( 0.6830127018922181881, 0.6830127018922202975, -0.2588190451025214056 ) ) ;
#19414=DIRECTION ( 'NONE',  ( -0.000000000000000000, 0.000000000000000000, 1.000000000000000000 ) ) ;
#19415=EDGE_CURVE ( 'NONE', #36287, #6138, #46906, .T. ) ;
#19416=DIRECTION ( 'NONE',  ( -1.000000000000000000, 0.000000000000000000, 0.000000000000000000 ) ) ;
#19419=LINE ( 'NONE', #107831, #129691 ) ;
#19420=DIRECTION ( 'NONE',  ( 0.7071067811865487940, 0.7071067811865463515, 0.000000000000000000 ) ) ;
#19421=ORIENTED_EDGE ( 'NONE', *, *, #31210, .T. ) ;
#19422=DIRECTION ( 'NONE',  ( 0.7071067811865487940, -0.7071067811865463515, 0.000000000000000000 ) ) ;
#19423=EDGE_CURVE ( 'NONE', #101030, #47360, #57038, .T. ) ;
#19425=ORIENTED_EDGE ( 'NONE', *, *, #69245, .F. ) ;
#19426=VECTOR ( 'NONE', #87177, 1000.000000000000227 ) ;
#19427=CARTESIAN_POINT ( 'NONE',  ( -25.49999999999982236, 21.05218569542895324, 5.000000000000000000 ) ) ;
#19429=EDGE_LOOP ( 'NONE', ( #46429, #139600, #23133, #116669 ) ) ;
#19430=VECTOR ( 'NONE', #142273, 1000.000000000000000 ) ;
#19431=CARTESIAN_POINT ( 'NONE',  ( -41.99451991528749062, 28.92564299267967343, 4.000000000000000000 ) ) ;
#19434=EDGE_CURVE ( 'NONE', #72893, #51489, #134589, .T. ) ;
#19435=EDGE_LOOP ( 'NONE', ( #86358, #47182, #125691, #122329 ) ) ;
#19436=LINE ( 'NONE', #32470, #109115 ) ;
#19437=EDGE_LOOP ( 'NONE', ( #31008, #130510, #1563, #135251 ) ) ;
#19441=CARTESIAN_POINT ( 'NONE',  ( 9.183988606268997046, 28.73617430169793607, 5.000000000000000000 ) ) ;
#19442=VECTOR ( 'NONE', #49194, 1000.000000000000114 ) ;
#19443=PLANE ( 'NONE',  #28265 ) ;
#19444=CARTESIAN_POINT ( 'NONE',  ( -25.49999999999981526, -7.912538124160678699, 4.000000000000000000 ) ) ;
#19445=EDGE_CURVE ( 'NONE', #35802, #138104, #101211, .T. ) ;
#19446=CARTESIAN_POINT ( 'NONE',  ( -32.20666063542130075, 21.75929247661549226, 4.998822639870715179 ) ) ;
#19451=LINE ( 'NONE', #18712, #73279 ) ;
#19452=ORIENTED_EDGE ( 'NONE', *, *, #69830, .F. ) ;
#19453=ADVANCED_FACE ( 'NONE', ( #113507 ), #459, .T. ) ;
#19454=EDGE_LOOP ( 'NONE', ( #57262, #47431, #73900, #45831 ) ) ;
#19455=EDGE_CURVE ( 'NONE', #96026, #111517, #58491, .T. ) ;
#19456=VECTOR ( 'NONE', #23463, 999.9999999999998863 ) ;
#19457=CARTESIAN_POINT ( 'NONE',  ( 5.999999999999967137, 8.587461875839155212, 4.000000000000000000 ) ) ;
#19458=VERTEX_POINT ( 'NONE', #78061 ) ;
#19459=CARTESIAN_POINT ( 'NONE',  ( 3.489213562373097322, -27.52281430457057709, 5.000000000000000000 ) ) ;
#19460=DIRECTION ( 'NONE',  ( 1.000000000000000000, -0.000000000000000000, 0.000000000000000000 ) ) ;
#19462=AXIS2_PLACEMENT_3D ( 'NONE', #110838, #89828, #123205 ) ;
#19465=CARTESIAN_POINT ( 'NONE',  ( -15.29974487139158867, -27.71228299555216879, 4.000000000000000000 ) ) ;
#19467=CARTESIAN_POINT ( 'NONE',  ( -11.99999999999992362, -6.108550654416973202, -3.114665004254993708 ) ) ;
#19468=EDGE_CURVE ( 'NONE', #2635, #75105, #90164, .T. ) ;
#19469=EDGE_CURVE ( 'NONE', #30259, #109556, #77191, .T. ) ;
#19471=PLANE ( 'NONE',  #72951 ) ;
#19472=ORIENTED_EDGE ( 'NONE', *, *, #109533, .F. ) ;
#19474=CARTESIAN_POINT ( 'NONE',  ( -32.99999999999975842, -13.39766691384885711, -10.96608748226458196 ) ) ;
#19475=DIRECTION ( 'NONE',  ( 0.7071067811865486830, -0.7071067811865464625, -0.000000000000000000 ) ) ;
#19476=LINE ( 'NONE', #119474, #93123 ) ;
#19478=ORIENTED_EDGE ( 'NONE', *, *, #343, .T. ) ;
#19479=ORIENTED_EDGE ( 'NONE', *, *, #100181, .T. ) ;
#19481=AXIS2_PLACEMENT_3D ( 'NONE', #19034, #106734, #84328 ) ;
#19483=EDGE_CURVE ( 'NONE', #79735, #49213, #24907, .T. ) ;
#19484=LINE ( 'NONE', #126803, #68607 ) ;
#19485=ORIENTED_EDGE ( 'NONE', *, *, #60393, .F. ) ;
#19488=LINE ( 'NONE', #110747, #11828 ) ;
#19491=EDGE_LOOP ( 'NONE', ( #94928, #3413, #81208, #89970 ) ) ;
#19492=CARTESIAN_POINT ( 'NONE',  ( 17.28242261357420517, -21.73023691814493219, 5.000000000000000888 ) ) ;
#19493=CARTESIAN_POINT ( 'NONE',  ( 0.000000000000000000, 0.000000000000000000, 5.000000000000000000 ) ) ;
#19494=DIRECTION ( 'NONE',  ( 0.7071067811865487940, 0.7071067811865463515, 0.000000000000000000 ) ) ;
#19495=DIRECTION ( 'NONE',  ( 1.000000000000000000, 0.000000000000000000, 0.000000000000000000 ) ) ;
#19496=ORIENTED_EDGE ( 'NONE', *, *, #82160, .T. ) ;
#19497=EDGE_LOOP ( 'NONE', ( #110195, #73196, #97372, #135675 ) ) ;
#19498=ORIENTED_EDGE ( 'NONE', *, *, #39453, .F. ) ;
#19499=CARTESIAN_POINT ( 'NONE',  ( 14.99999999999989519, -7.447814304570745669, 5.000000000000000000 ) ) ;
#19500=DIRECTION ( 'NONE',  ( 0.3543493200069162685, -0.000000000000000000, -0.9351131265310288487 ) ) ;
#19502=VECTOR ( 'NONE', #17733, 1000.000000000000000 ) ;
#19503=CARTESIAN_POINT ( 'NONE',  ( -77.99451991528749772, 28.92564299267992567, 4.000000000000000000 ) ) ;
#19505=EDGE_CURVE ( 'NONE', #119204, #21635, #35834, .T. ) ;
#19507=ADVANCED_FACE ( 'NONE', ( #1000 ), #101035, .F. ) ;
#19508=VECTOR ( 'NONE', #7492, 1000.000000000000227 ) ;
#19510=VERTEX_POINT ( 'NONE', #90912 ) ;
#19511=VECTOR ( 'NONE', #20693, 1000.000000000000000 ) ;
#19514=ORIENTED_EDGE ( 'NONE', *, *, #59293, .T. ) ;
#19515=EDGE_CURVE ( 'NONE', #8278, #81137, #45982, .T. ) ;
#19516=PLANE ( 'NONE',  #83612 ) ;
#19517=CARTESIAN_POINT ( 'NONE',  ( 56.99451991528749062, 28.92564299267978001, 4.000000000000000000 ) ) ;
#19518=ORIENTED_EDGE ( 'NONE', *, *, #133090, .F. ) ;
#19521=CARTESIAN_POINT ( 'NONE',  ( -39.29974487139159578, -27.71228299555233576, 4.000000000000000000 ) ) ;
#19522=DIRECTION ( 'NONE',  ( 0.000000000000000000, 0.000000000000000000, 1.000000000000000000 ) ) ;
#19523=( BOUNDED_CURVE ( )  B_SPLINE_CURVE ( 3, ( #32333, #97566, #64243, #1093 ),
 .UNSPECIFIED., .F., .T. ) 
 B_SPLINE_CURVE_WITH_KNOTS ( ( 4, 4 ),
 ( 1.208578181583239486, 1.359146454359483336 ),
 .UNSPECIFIED. ) 
 CURVE ( )  GEOMETRIC_REPRESENTATION_ITEM ( )  RATIONAL_B_SPLINE_CURVE ( ( 1.000000000000000000, 0.9981116584018941973, 0.9981116584018941973, 1.000000000000000000 ) ) 
 REPRESENTATION_ITEM ( '' )  );
#19524=DIRECTION ( 'NONE',  ( -0.7071067811865486830, -0.7071067811865464625, -0.000000000000000000 ) ) ;
#19527=CARTESIAN_POINT ( 'NONE',  ( -8.218373117075001844, 21.74787736706806385, 4.999607392498049308 ) ) ;
#19529=ORIENTED_EDGE ( 'NONE', *, *, #58261, .F. ) ;
#19531=LINE ( 'NONE', #42018, #11009 ) ;
#19532=VERTEX_POINT ( 'NONE', #123552 ) ;
#19533=VERTEX_POINT ( 'NONE', #57573 ) ;
#19534=LINE ( 'NONE', #85487, #117593 ) ;
#19535=ORIENTED_EDGE ( 'NONE', *, *, #113801, .F. ) ;
#19536=EDGE_LOOP ( 'NONE', ( #122, #77542, #92761, #82854 ) ) ;
#19537=ORIENTED_EDGE ( 'NONE', *, *, #43585, .T. ) ;
#19541=VECTOR ( 'NONE', #78270, 1000.000000000000000 ) ;
#19542=DIRECTION ( 'NONE',  ( 0.7071067811865487940, 0.7071067811865463515, 0.000000000000000000 ) ) ;
#19543=DIRECTION ( 'NONE',  ( -0.000000000000000000, 0.3543493200069153248, 0.9351131265310292928 ) ) ;
#19544=CARTESIAN_POINT ( 'NONE',  ( 24.43680103220814104, -12.74070752338415780, 9.898150129686316134 ) ) ;
#19545=ADVANCED_FACE ( 'NONE', ( #24215 ), #68461, .F. ) ;
#19546=DIRECTION ( 'NONE',  ( -0.3543493200069162685, -0.000000000000000000, -0.9351131265310288487 ) ) ;
#19547=PLANE ( 'NONE',  #53921 ) ;
#19548=AXIS2_PLACEMENT_3D ( 'NONE', #82322, #92435, #117748 ) ;
#19549=CARTESIAN_POINT ( 'NONE',  ( 21.78162688292479743, 21.74787736706806029, 4.999607392498049308 ) ) ;
#19550=LINE ( 'NONE', #63796, #25207 ) ;
#19551=FACE_OUTER_BOUND ( 'NONE', #125075, .T. ) ;
#19552=VERTEX_POINT ( 'NONE', #47441 ) ;
#19553=VERTEX_POINT ( 'NONE', #124229 ) ;
#19555=ORIENTED_EDGE ( 'NONE', *, *, #111827, .T. ) ;
#19556=LINE ( 'NONE', #63802, #42556 ) ;
#19557=ORIENTED_EDGE ( 'NONE', *, *, #36160, .F. ) ;
#19558=EDGE_CURVE ( 'NONE', #21017, #43833, #58320, .T. ) ;
#19559=VERTEX_POINT ( 'NONE', #60433 ) ;
#19560=DIRECTION ( 'NONE',  ( 1.000000000000000000, 0.000000000000000000, 0.000000000000000000 ) ) ;
#19562=ADVANCED_FACE ( 'NONE', ( #27766 ), #25618, .T. ) ;
#19563=EDGE_CURVE ( 'NONE', #8278, #80300, #19243, .T. ) ;
#19564=FACE_OUTER_BOUND ( 'NONE', #108313, .T. ) ;
#19566=VERTEX_POINT ( 'NONE', #124936 ) ;
#19567=CARTESIAN_POINT ( 'NONE',  ( -24.48921356237309510, -27.52281430457072631, 5.000000000000000000 ) ) ;
#19568=EDGE_CURVE ( 'NONE', #106128, #81473, #15425, .T. ) ;
#19569=ADVANCED_FACE ( 'NONE', ( #116210 ), #103873, .T. ) ;
#19570=CARTESIAN_POINT ( 'NONE',  ( 0.000000000000000000, 0.000000000000000000, 5.000000000000000000 ) ) ;
#19572=ORIENTED_EDGE ( 'NONE', *, *, #18793, .T. ) ;
#19575=EDGE_CURVE ( 'NONE', #12595, #139718, #49562, .T. ) ;
#19576=LINE ( 'NONE', #63819, #48696 ) ;
#19577=PLANE ( 'NONE',  #58146 ) ;
#19579=ORIENTED_EDGE ( 'NONE', *, *, #61115, .F. ) ;
#19580=LINE ( 'NONE', #57777, #82084 ) ;
#19582=CARTESIAN_POINT ( 'NONE',  ( 33.70701326429281153, -21.74070752338406365, 4.999753212805220670 ) ) ;
#19583=CARTESIAN_POINT ( 'NONE',  ( 29.99451991528749417, 28.92564299267958816, 4.000000000000000000 ) ) ;
#19584=CARTESIAN_POINT ( 'NONE',  ( -30.48921356237309510, -27.52281430457076894, 5.000000000000000000 ) ) ;
#19585=DIRECTION ( 'NONE',  ( 0.6830127018922180770, -0.6830127018922204085, -0.2588190451025213501 ) ) ;
#19586=AXIS2_PLACEMENT_3D ( 'NONE', #59350, #135472, #4146 ) ;
#19587=ORIENTED_EDGE ( 'NONE', *, *, #105580, .F. ) ;
#19588=FACE_OUTER_BOUND ( 'NONE', #140426, .T. ) ;
#19589=ADVANCED_FACE ( 'NONE', ( #94443 ), #82191, .F. ) ;
#19590=PLANE ( 'NONE',  #102213 ) ;
#19591=CARTESIAN_POINT ( 'NONE',  ( -20.99999999999985079, -9.412538124160658271, 4.000000000000000000 ) ) ;
#19593=CARTESIAN_POINT ( 'NONE',  ( 3.489213562373097322, -27.52281430457057709, 5.000000000000000000 ) ) ;
#19594=EDGE_CURVE ( 'NONE', #18836, #47983, #16901, .T. ) ;
#19595=DIRECTION ( 'NONE',  ( -1.000000000000000000, 0.000000000000000000, 0.000000000000000000 ) ) ;
#19596=ORIENTED_EDGE ( 'NONE', *, *, #81058, .F. ) ;
#19598=ORIENTED_EDGE ( 'NONE', *, *, #22169, .T. ) ;
#19599=EDGE_LOOP ( 'NONE', ( #50422, #137937, #4573 ) ) ;
#19601=CARTESIAN_POINT ( 'NONE',  ( -10.49999999999992539, 12.05218569542904561, 5.000000000000000000 ) ) ;
#19603=EDGE_CURVE ( 'NONE', #17066, #44633, #50254, .T. ) ;
#19605=PLANE ( 'NONE',  #220 ) ;
#19606=DIRECTION ( 'NONE',  ( 0.3543493200069162685, -0.000000000000000000, -0.9351131265310288487 ) ) ;
#19607=VECTOR ( 'NONE', #87049, 1000.000000000000000 ) ;
#19608=CARTESIAN_POINT ( 'NONE',  ( -27.46160355370554029, -9.740707523384173783, 17.74957260769604517 ) ) ;
#19609=LINE ( 'NONE', #63857, #90120 ) ;
#19612=CARTESIAN_POINT ( 'NONE',  ( 36.48921356237310221, -27.52281430457080802, 5.000000000000000000 ) ) ;
#19613=CARTESIAN_POINT ( 'NONE',  ( 23.20710678118638626, 12.75929247661558996, 5.000000000000000000 ) ) ;
#19615=DIRECTION ( 'NONE',  ( 0.6830127018922180770, -0.6830127018922204085, -0.2588190451025213501 ) ) ;
#19616=CARTESIAN_POINT ( 'NONE',  ( 8.277185695429338352, -21.72500000000000142, 5.000000000000000000 ) ) ;
#19617=DIRECTION ( 'NONE',  ( -0.7071067811865486830, -0.7071067811865464625, 0.000000000000000000 ) ) ;
#19618=LINE ( 'NONE', #66017, #129335 ) ;
#19620=CARTESIAN_POINT ( 'NONE',  ( 28.49999999999980460, -9.462702396500981550, -9.474982329943578918 ) ) ;
#19623=ORIENTED_EDGE ( 'NONE', *, *, #92384, .F. ) ;
#19624=EDGE_CURVE ( 'NONE', #61647, #36536, #126361, .T. ) ;
#19626=ORIENTED_EDGE ( 'NONE', *, *, #30400, .T. ) ;
#19627=VECTOR ( 'NONE', #106960, 1000.000000000000000 ) ;
#19628=VERTEX_POINT ( 'NONE', #3825 ) ;
#19629=EDGE_CURVE ( 'NONE', #136190, #51950, #17585, .T. ) ;
#19630=ORIENTED_EDGE ( 'NONE', *, *, #66567, .F. ) ;
#19631=CARTESIAN_POINT ( 'NONE',  ( -34.92500000000001137, -22.22500000000000142, 4.500000000000000888 ) ) ;
#19632=CARTESIAN_POINT ( 'NONE',  ( -26.29289321881326913, 8.259292476615634371, 5.000000000000000000 ) ) ;
#19634=DIRECTION ( 'NONE',  ( -0.7071067811865486830, -0.7071067811865464625, -0.000000000000000000 ) ) ;
#19635=EDGE_CURVE ( 'NONE', #89978, #105099, #136518, .T. ) ;
#19636=DIRECTION ( 'NONE',  ( 0.6830127018922180770, -0.6830127018922204085, -0.2588190451025213501 ) ) ;
#19637=LINE ( 'NONE', #110901, #16272 ) ;
#19638=CARTESIAN_POINT ( 'NONE',  ( 27.48921356237309155, -27.52281430457074762, 5.000000000000000000 ) ) ;
#19640=ORIENTED_EDGE ( 'NONE', *, *, #64624, .F. ) ;
#19641=CARTESIAN_POINT ( 'NONE',  ( 0.7928932188134563130, -11.24070752338416668, 5.000000000000000000 ) ) ;
#19642=LINE ( 'NONE', #40009, #72864 ) ;
#19643=DIRECTION ( 'NONE',  ( 0.7071067811865486830, -0.7071067811865464625, -0.000000000000000000 ) ) ;
#19644=CARTESIAN_POINT ( 'NONE',  ( 13.49999999999991296, 12.05218569542904561, 5.000000000000000000 ) ) ;
#19645=CARTESIAN_POINT ( 'NONE',  ( -2.994519915287485734, 28.92564299267940342, 4.000000000000000000 ) ) ;
#19646=LINE ( 'NONE', #141434, #89291 ) ;
#19647=AXIS2_PLACEMENT_3D ( 'NONE', #110549, #133766, #22123 ) ;
#19648=CARTESIAN_POINT ( 'NONE',  ( -27.48921356237309155, -27.52281430457074762, 5.000000000000000000 ) ) ;
#19649=VECTOR ( 'NONE', #23301, 1000.000000000000227 ) ;
#19650=EDGE_LOOP ( 'NONE', ( #97032, #111590, #37336, #27979 ) ) ;
#19651=VERTEX_POINT ( 'NONE', #6683 ) ;
#19652=VECTOR ( 'NONE', #136882, 1000.000000000000227 ) ;
#19654=ORIENTED_EDGE ( 'NONE', *, *, #44570, .T. ) ;
#19655=VECTOR ( 'NONE', #55025, 1000.000000000000000 ) ;
#19656=ADVANCED_FACE ( 'NONE', ( #91603 ), #104614, .F. ) ;
#19658=LINE ( 'NONE', #121804, #66378 ) ;
#19659=CARTESIAN_POINT ( 'NONE',  ( 34.75611968250419181, -19.29434930147575500, 4.955485411084881164 ) ) ;
#19660=EDGE_CURVE ( 'NONE', #128218, #26178, #71298, .T. ) ;
#19661=CARTESIAN_POINT ( 'NONE',  ( 14.81601139373099585, 28.73617430169776910, 5.000000000000000000 ) ) ;
#19666=ORIENTED_EDGE ( 'NONE', *, *, #8166, .F. ) ;
#19669=LINE ( 'NONE', #9477, #90735 ) ;
#19670=VERTEX_POINT ( 'NONE', #125673 ) ;
#19671=EDGE_CURVE ( 'NONE', #63574, #52633, #81472, .T. ) ;
#19674=DIRECTION ( 'NONE',  ( -0.7071067811865487940, 0.7071067811865463515, -0.000000000000000000 ) ) ;
#19676=PLANE ( 'NONE',  #61787 ) ;
#19678=ADVANCED_FACE ( 'NONE', ( #127075 ), #7421, .F. ) ;
#19680=ORIENTED_EDGE ( 'NONE', *, *, #47251, .T. ) ;
#19681=DIRECTION ( 'NONE',  ( -0.7071067811865487940, 0.7071067811865463515, -0.000000000000000000 ) ) ;
#19682=VERTEX_POINT ( 'NONE', #107465 ) ;
#19683=ORIENTED_EDGE ( 'NONE', *, *, #14347, .F. ) ;
#19685=EDGE_CURVE ( 'NONE', #45742, #130861, #76841, .T. ) ;
#19686=EDGE_CURVE ( 'NONE', #117528, #121710, #22391, .T. ) ;
#19687=CARTESIAN_POINT ( 'NONE',  ( -42.48921356237308800, -27.52281430457085065, 5.000000000000000000 ) ) ;
#19688=ORIENTED_EDGE ( 'NONE', *, *, #100798, .T. ) ;
#19689=CARTESIAN_POINT ( 'NONE',  ( -12.29974487139158512, -27.71228299555214747, 4.000000000000000000 ) ) ;
#19690=LINE ( 'NONE', #28454, #31705 ) ;
#19691=CYLINDRICAL_SURFACE ( 'NONE', #124663, 0.5000000000000004441 ) ;
#19693=FACE_BOUND ( 'NONE', #99059, .T. ) ;
#19694=EDGE_LOOP ( 'NONE', ( #101159, #65643, #90517, #16740 ) ) ;
#19695=ADVANCED_FACE ( 'NONE', ( #29896 ), #23100, .T. ) ;
#19696=CARTESIAN_POINT ( 'NONE',  ( -15.48921356237309510, -27.52281430457066236, 5.000000000000000000 ) ) ;
#19697=LINE ( 'NONE', #42197, #18979 ) ;
#19698=DIRECTION ( 'NONE',  ( -0.000000000000000000, 0.3543493200069153248, 0.9351131265310292928 ) ) ;
#19699=ORIENTED_EDGE ( 'NONE', *, *, #11688, .T. ) ;
#19701=ORIENTED_EDGE ( 'NONE', *, *, #82221, .T. ) ;
#19702=ORIENTED_EDGE ( 'NONE', *, *, #77580, .T. ) ;
#19703=LINE ( 'NONE', #86417, #40240 ) ;
#19704=( BOUNDED_CURVE ( )  B_SPLINE_CURVE ( 3, ( #132698, #110864, #143527, #121052 ),
 .UNSPECIFIED., .F., .T. ) 
 B_SPLINE_CURVE_WITH_KNOTS ( ( 4, 4 ),
 ( 1.964434688349486313, 3.503810798801452187 ),
 .UNSPECIFIED. ) 
 CURVE ( )  GEOMETRIC_REPRESENTATION_ITEM ( )  RATIONAL_B_SPLINE_CURVE ( ( 1.000000000000000000, 0.8120851936182275077, 0.8120851936182275077, 1.000000000000000000 ) ) 
 REPRESENTATION_ITEM ( '' )  );
#19705=VERTEX_POINT ( 'NONE', #128526 ) ;
#19706=VECTOR ( 'NONE', #84054, 1000.000000000000227 ) ;
#19708=ORIENTED_EDGE ( 'NONE', *, *, #20399, .T. ) ;
#19709=CARTESIAN_POINT ( 'NONE',  ( 22.49999999999984368, -12.66682484999664204, -0.6294897503863420285 ) ) ;
#19711=ORIENTED_EDGE ( 'NONE', *, *, #11241, .F. ) ;
#19713=CARTESIAN_POINT ( 'NONE',  ( 28.49999999999980460, -1.592773361805344789, -6.492772025301293937 ) ) ;
#19714=DIRECTION ( 'NONE',  ( 0.7071067811865487940, 0.7071067811865463515, 0.000000000000000000 ) ) ;
#19715=VECTOR ( 'NONE', #4209, 1000.000000000000000 ) ;
#19716=PLANE ( 'NONE',  #101450 ) ;
#19718=LINE ( 'NONE', #54524, #44699 ) ;
#19719=CARTESIAN_POINT ( 'NONE',  ( -1.499999999999990896, 11.52377502935403264, -1.522421517564079618 ) ) ;
#19720=EDGE_LOOP ( 'NONE', ( #66178, #120470, #96565, #114117 ) ) ;
#19721=EDGE_CURVE ( 'NONE', #66027, #114208, #110823, .T. ) ;
#19722=EDGE_LOOP ( 'NONE', ( #90445, #128985, #23300, #46375 ) ) ;
#19723=CARTESIAN_POINT ( 'NONE',  ( -27.77004279457773706, 21.73644205237998506, 5.000000000000000888 ) ) ;
#19725=ORIENTED_EDGE ( 'NONE', *, *, #26345, .F. ) ;
#19726=VERTEX_POINT ( 'NONE', #132658 ) ;
#19728=FACE_OUTER_BOUND ( 'NONE', #7781, .T. ) ;
#19729=DIRECTION ( 'NONE',  ( -1.000000000000000000, 0.000000000000000000, -0.000000000000000000 ) ) ;
#19730=ADVANCED_FACE ( 'NONE', ( #29191 ), #74138, .F. ) ;
#19731=ADVANCED_FACE ( 'NONE', ( #99994 ), #10802, .F. ) ;
#19732=EDGE_CURVE ( 'NONE', #50892, #68263, #96556, .T. ) ;
#19733=LINE ( 'NONE', #129939, #124954 ) ;
#19734=ORIENTED_EDGE ( 'NONE', *, *, #60095, .F. ) ;
#19735=LINE ( 'NONE', #108146, #87986 ) ;
#19736=VECTOR ( 'NONE', #91191, 999.9999999999998863 ) ;
#19737=DIRECTION ( 'NONE',  ( -0.3543493200069162685, -0.000000000000000000, -0.9351131265310288487 ) ) ;
#19739=EDGE_CURVE ( 'NONE', #37058, #18032, #95875, .T. ) ;
#19740=AXIS2_PLACEMENT_3D ( 'NONE', #140972, #7599, #51863 ) ;
#19742=VECTOR ( 'NONE', #26440, 999.9999999999998863 ) ;
#19744=EDGE_LOOP ( 'NONE', ( #13574, #46399, #79150, #27519 ) ) ;
#19746=VECTOR ( 'NONE', #81834, 1000.000000000000227 ) ;
#19747=EDGE_CURVE ( 'NONE', #59289, #96641, #67383, .T. ) ;
#19748=CARTESIAN_POINT ( 'NONE',  ( 14.29289321881335795, 17.25929247661554911, 5.000000000000000000 ) ) ;
#19749=CARTESIAN_POINT ( 'NONE',  ( -13.49999999999990763, -4.216083040037257312, -7.486842126848625156 ) ) ;
#19750=CARTESIAN_POINT ( 'NONE',  ( 75.18398860626899705, 28.73617430169839793, 5.000000000000000000 ) ) ;
#19751=ORIENTED_EDGE ( 'NONE', *, *, #83638, .F. ) ;
#19752=FACE_OUTER_BOUND ( 'NONE', #15177, .T. ) ;
#19753=VERTEX_POINT ( 'NONE', #88416 ) ;
#19755=CARTESIAN_POINT ( 'NONE',  ( 0.6549448374538157092, 5.259292476615669010, 12.77922209995893965 ) ) ;
#19757=LINE ( 'NONE', #19047, #98183 ) ;
#19758=VERTEX_POINT ( 'NONE', #95157 ) ;
#19759=EDGE_CURVE ( 'NONE', #142885, #91787, #11510, .T. ) ;
#19761=CARTESIAN_POINT ( 'NONE',  ( -23.58838509405152806, 22.22500000000000142, 4.777194822843820354 ) ) ;
#19762=ORIENTED_EDGE ( 'NONE', *, *, #140990, .T. ) ;
#19763=LINE ( 'NONE', #66153, #27698 ) ;
#19764=EDGE_LOOP ( 'NONE', ( #6918, #97120, #36535, #70855 ) ) ;
#19765=EDGE_CURVE ( 'NONE', #90132, #47491, #18285, .T. ) ;
#19768=ORIENTED_EDGE ( 'NONE', *, *, #52172, .T. ) ;
#19770=LINE ( 'NONE', #75601, #47334 ) ;
#19772=EDGE_CURVE ( 'NONE', #77649, #94584, #32607, .T. ) ;
#19774=CARTESIAN_POINT ( 'NONE',  ( -33.72281430457037743, -21.72499999999999432, 5.000000000000000000 ) ) ;
#19775=CARTESIAN_POINT ( 'NONE',  ( -57.48921356237308800, -27.52281430457095368, 5.000000000000000000 ) ) ;
#19776=DIRECTION ( 'NONE',  ( -0.000000000000000000, -0.3543493200069152693, 0.9351131265310292928 ) ) ;
#19777=ORIENTED_EDGE ( 'NONE', *, *, #26301, .F. ) ;
#19779=CARTESIAN_POINT ( 'NONE',  ( -60.48921356237309510, -27.52281430457097500, 5.000000000000000000 ) ) ;
#19780=DIRECTION ( 'NONE',  ( 0.7071067811865486830, -0.7071067811865464625, -0.000000000000000000 ) ) ;
#19783=PLANE ( 'NONE',  #81139 ) ;
#19785=EDGE_CURVE ( 'NONE', #23904, #75615, #85001, .T. ) ;
#19786=CARTESIAN_POINT ( 'NONE',  ( -15.18398860626900237, 28.73617430169797871, 5.000000000000000000 ) ) ;
#19787=ORIENTED_EDGE ( 'NONE', *, *, #63774, .T. ) ;
#19789=ORIENTED_EDGE ( 'NONE', *, *, #76291, .T. ) ;
#19790=CARTESIAN_POINT ( 'NONE',  ( -18.60241805642224122, 22.22500000000000142, -1.185236468576118085 ) ) ;
#19791=FACE_OUTER_BOUND ( 'NONE', #126340, .T. ) ;
#19792=EDGE_LOOP ( 'NONE', ( #14608, #19007, #112317, #32842 ) ) ;
#19793=EDGE_CURVE ( 'NONE', #80757, #45698, #89812, .T. ) ;
#19794=DIRECTION ( 'NONE',  ( 1.000000000000000000, 0.000000000000000000, 0.000000000000000000 ) ) ;
#19796=LINE ( 'NONE', #106797, #127387 ) ;
#19798=LINE ( 'NONE', #64038, #107865 ) ;
#19799=VERTEX_POINT ( 'NONE', #126037 ) ;
#19800=PLANE ( 'NONE',  #134818 ) ;
#19801=PLANE ( 'NONE',  #102833 ) ;
#19803=FACE_OUTER_BOUND ( 'NONE', #48331, .T. ) ;
#19804=EDGE_CURVE ( 'NONE', #57991, #39522, #13658, .T. ) ;
#19805=DIRECTION ( 'NONE',  ( -0.7071067811865486830, -0.7071067811865464625, 0.000000000000000000 ) ) ;
#19807=AXIS2_PLACEMENT_3D ( 'NONE', #118431, #96648, #115546 ) ;
#19808=DIRECTION ( 'NONE',  ( -0.6830127018922181881, 0.6830127018922202975, -0.2588190451025214056 ) ) ;
#19809=ORIENTED_EDGE ( 'NONE', *, *, #87652, .F. ) ;
#19810=VERTEX_POINT ( 'NONE', #1355 ) ;
#19814=EDGE_CURVE ( 'NONE', #76846, #26526, #114371, .T. ) ;
#19815=DIRECTION ( 'NONE',  ( -0.7071067811865486830, -0.7071067811865464625, 0.000000000000000000 ) ) ;
#19816=DIRECTION ( 'NONE',  ( 0.7071067811865487940, 0.7071067811865463515, -0.000000000000000000 ) ) ;
#19818=CARTESIAN_POINT ( 'NONE',  ( 2.683420388672089985, -6.740707523384216415, 11.88629033278123792 ) ) ;
#19820=VERTEX_POINT ( 'NONE', #12953 ) ;
#19821=CARTESIAN_POINT ( 'NONE',  ( 34.45011844616453800, -10.48371918836239125, 5.000000000000001776 ) ) ;
#19822=ORIENTED_EDGE ( 'NONE', *, *, #12432, .F. ) ;
#19823=ORIENTED_EDGE ( 'NONE', *, *, #15035, .F. ) ;
#19824=CARTESIAN_POINT ( 'NONE',  ( -27.48921356237309155, -27.52281430457074762, 5.000000000000000000 ) ) ;
#19828=VERTEX_POINT ( 'NONE', #70268 ) ;
#19829=EDGE_CURVE ( 'NONE', #3009, #98945, #102145, .T. ) ;
#19830=FACE_OUTER_BOUND ( 'NONE', #114576, .T. ) ;
#19831=LINE ( 'NONE', #101504, #114696 ) ;
#19832=ORIENTED_EDGE ( 'NONE', *, *, #63238, .F. ) ;
#19834=CARTESIAN_POINT ( 'NONE',  ( 2.816011393730999401, 28.73617430169785436, 5.000000000000000000 ) ) ;
#19835=CARTESIAN_POINT ( 'NONE',  ( 28.49999999999981171, -1.533600742197719580, 5.000000000000000000 ) ) ;
#19836=CARTESIAN_POINT ( 'NONE',  ( -17.99451991528748351, 28.92564299267950645, 4.000000000000000000 ) ) ;
#19837=LINE ( 'NONE', #140900, #127331 ) ;
#19838=LINE ( 'NONE', #53184, #131906 ) ;
#19839=VECTOR ( 'NONE', #39662, 1000.000000000000000 ) ;
#19840=EDGE_CURVE ( 'NONE', #129197, #49512, #124593, .T. ) ;
#19842=VERTEX_POINT ( 'NONE', #26002 ) ;
#19844=CARTESIAN_POINT ( 'NONE',  ( -19.05000000000000071, 3.174999999999997158, 5.000000000000000000 ) ) ;
#19846=LINE ( 'NONE', #141652, #60407 ) ;
#19847=FACE_OUTER_BOUND ( 'NONE', #130936, .T. ) ;
#19848=LINE ( 'NONE', #8920, #96577 ) ;
#19849=VERTEX_POINT ( 'NONE', #57951 ) ;
#19850=ORIENTED_EDGE ( 'NONE', *, *, #91179, .F. ) ;
#19851=VECTOR ( 'NONE', #119962, 1000.000000000000000 ) ;
#19852=DIRECTION ( 'NONE',  ( 0.6830127018922180770, -0.6830127018922204085, -0.2588190451025213501 ) ) ;
#19854=ORIENTED_EDGE ( 'NONE', *, *, #18437, .T. ) ;
#19855=EDGE_CURVE ( 'NONE', #42001, #94991, #26706, .T. ) ;
#19856=ORIENTED_EDGE ( 'NONE', *, *, #29130, .T. ) ;
#19857=EDGE_CURVE ( 'NONE', #113212, #8140, #123187, .T. ) ;
#19858=LINE ( 'NONE', #55370, #72261 ) ;
#19859=ORIENTED_EDGE ( 'NONE', *, *, #80033, .T. ) ;
#19860=CARTESIAN_POINT ( 'NONE',  ( 18.15612307739229081, -22.22500000000000142, 4.000000000000000000 ) ) ;
#19861=LINE ( 'NONE', #30772, #15552 ) ;
#19863=FACE_BOUND ( 'NONE', #132562, .T. ) ;
#19864=EDGE_CURVE ( 'NONE', #46897, #96881, #80399, .T. ) ;
#19865=FACE_OUTER_BOUND ( 'NONE', #118913, .T. ) ;
#19867=LINE ( 'NONE', #64828, #68820 ) ;
#19868=LINE ( 'NONE', #8945, #92147 ) ;
#19869=ORIENTED_EDGE ( 'NONE', *, *, #106004, .F. ) ;
#19870=DIRECTION ( 'NONE',  ( -0.7071067811865486830, -0.7071067811865464625, 0.000000000000000000 ) ) ;
#19874=EDGE_LOOP ( 'NONE', ( #84755, #105957, #108645, #135459 ) ) ;
#19875=FACE_OUTER_BOUND ( 'NONE', #46866, .T. ) ;
#19876=FACE_OUTER_BOUND ( 'NONE', #107929, .T. ) ;
#19877=ORIENTED_EDGE ( 'NONE', *, *, #73535, .F. ) ;
#19878=CARTESIAN_POINT ( 'NONE',  ( -31.49999999999977973, 19.39370406404964697, 1.459788787078273753 ) ) ;
#19880=CARTESIAN_POINT ( 'NONE',  ( -22.43312800248727967, -21.74070752338406010, 6.915939825044126188 ) ) ;
#19881=CARTESIAN_POINT ( 'NONE',  ( 12.18398860626900060, 28.73617430169795739, 5.000000000000000000 ) ) ;
#19883=FACE_OUTER_BOUND ( 'NONE', #30071, .T. ) ;
#19884=LINE ( 'NONE', #63446, #86370 ) ;
#19885=CARTESIAN_POINT ( 'NONE',  ( -28.82816939922332011, 18.75929247661552779, 4.000000000000000000 ) ) ;
#19886=EDGE_LOOP ( 'NONE', ( #35198, #92694, #86276, #126892 ) ) ;
#19887=DIRECTION ( 'NONE',  ( 0.7071067811865487940, -0.7071067811865463515, 0.000000000000000000 ) ) ;
#19888=VERTEX_POINT ( 'NONE', #2800 ) ;
#19889=LINE ( 'NONE', #84477, #10186 ) ;
#19890=DIRECTION ( 'NONE',  ( 0.7071067811865487940, 0.7071067811865463515, 0.000000000000000000 ) ) ;
#19891=ORIENTED_EDGE ( 'NONE', *, *, #138410, .T. ) ;
#19892=ORIENTED_EDGE ( 'NONE', *, *, #80883, .F. ) ;
#19893=VERTEX_POINT ( 'NONE', #114425 ) ;
#19895=ORIENTED_EDGE ( 'NONE', *, *, #5053, .F. ) ;
#19897=VECTOR ( 'NONE', #141263, 1000.000000000000000 ) ;
#19898=EDGE_CURVE ( 'NONE', #14772, #26574, #134790, .T. ) ;
#19901=ADVANCED_FACE ( 'NONE', ( #81844 ), #58686, .T. ) ;
#19902=VERTEX_POINT ( 'NONE', #68125 ) ;
#19904=FACE_OUTER_BOUND ( 'NONE', #72633, .T. ) ;
#19905=EDGE_CURVE ( 'NONE', #74597, #109521, #12252, .T. ) ;
#19907=CARTESIAN_POINT ( 'NONE',  ( 39.29974487139159578, -27.71228299555233576, 4.000000000000000000 ) ) ;
#19908=DIRECTION ( 'NONE',  ( 0.000000000000000000, -0.3543493200069153248, -0.9351131265310291818 ) ) ;
#19909=LINE ( 'NONE', #108319, #79608 ) ;
#19910=EDGE_LOOP ( 'NONE', ( #100919, #24405, #30412, #138541 ) ) ;
#19911=ORIENTED_EDGE ( 'NONE', *, *, #41416, .F. ) ;
#19912=EDGE_CURVE ( 'NONE', #114730, #125554, #101404, .T. ) ;
#19913=( BOUNDED_CURVE ( )  B_SPLINE_CURVE ( 3, ( #80333, #124522, #58612, #102784 ),
 .UNSPECIFIED., .F., .F. ) 
 B_SPLINE_CURVE_WITH_KNOTS ( ( 4, 4 ),
 ( 1.964434688349490532, 3.503810798801449522 ),
 .UNSPECIFIED. ) 
 CURVE ( )  GEOMETRIC_REPRESENTATION_ITEM ( )  RATIONAL_B_SPLINE_CURVE ( ( 1.000000000000000000, 0.8120851936182292841, 0.8120851936182292841, 1.000000000000000000 ) ) 
 REPRESENTATION_ITEM ( '' )  );
#19914=DIRECTION ( 'NONE',  ( -0.000000000000000000, 0.3543493200069153248, 0.9351131265310292928 ) ) ;
#19915=DIRECTION ( 'NONE',  ( 0.3543493200069162685, -0.000000000000000000, -0.9351131265310288487 ) ) ;
#19916=ORIENTED_EDGE ( 'NONE', *, *, #108484, .T. ) ;
#19918=EDGE_LOOP ( 'NONE', ( #120774, #85903, #137024, #19237 ) ) ;
#19920=VERTEX_POINT ( 'NONE', #35486 ) ;
#19921=VECTOR ( 'NONE', #5752, 1000.000000000000227 ) ;
#19922=ADVANCED_FACE ( 'NONE', ( #56537 ), #68814, .F. ) ;
#19923=DIRECTION ( 'NONE',  ( 0.6830127018922180770, -0.6830127018922204085, -0.2588190451025213501 ) ) ;
#19924=LINE ( 'NONE', #99623, #64662 ) ;
#19925=DIRECTION ( 'NONE',  ( -0.3543493200069162685, -0.000000000000000000, -0.9351131265310288487 ) ) ;
#19927=EDGE_CURVE ( 'NONE', #63317, #33976, #100712, .T. ) ;
#19928=CARTESIAN_POINT ( 'NONE',  ( -23.81601139373100295, 28.73617430169770870, 5.000000000000000000 ) ) ;
#19929=CARTESIAN_POINT ( 'NONE',  ( -34.49999999999975131, 19.46425560840030400, 4.994342998332171213 ) ) ;
#19930=EDGE_CURVE ( 'NONE', #27059, #67630, #47098, .T. ) ;
#19932=DIRECTION ( 'NONE',  ( -0.6830127018922181881, 0.6830127018922202975, -0.2588190451025214056 ) ) ;
#19933=ORIENTED_EDGE ( 'NONE', *, *, #4077, .T. ) ;
#19935=EDGE_CURVE ( 'NONE', #22706, #58114, #128864, .T. ) ;
#19936=AXIS2_PLACEMENT_3D ( 'NONE', #111112, #11803, #56090 ) ;
#19937=CARTESIAN_POINT ( 'NONE',  ( 59.99451991528749772, 28.92564299267980132, 4.000000000000000000 ) ) ;
#19938=AXIS2_PLACEMENT_3D ( 'NONE', #15159, #123965, #103596 ) ;
#19939=ORIENTED_EDGE ( 'NONE', *, *, #123751, .F. ) ;
#19940=CARTESIAN_POINT ( 'NONE',  ( 0.000000000000000000, 0.000000000000000000, 5.000000000000000000 ) ) ;
#19941=CARTESIAN_POINT ( 'NONE',  ( 2.999999999999992450, -19.44781430457064175, 5.000000000000000000 ) ) ;
#19942=ORIENTED_EDGE ( 'NONE', *, *, #25430, .T. ) ;
#19943=AXIS2_PLACEMENT_3D ( 'NONE', #126968, #27659, #22474 ) ;
#19945=CARTESIAN_POINT ( 'NONE',  ( 6.813491353976342424, -15.74070752338412049, 8.904080028138924519 ) ) ;
#19949=VECTOR ( 'NONE', #114470, 1000.000000000000000 ) ;
#19950=DIRECTION ( 'NONE',  ( 1.000000000000000000, 0.000000000000000000, 0.000000000000000000 ) ) ;
#19951=DIRECTION ( 'NONE',  ( -0.000000000000000000, -0.3543493200069152693, 0.9351131265310292928 ) ) ;
#19953=LINE ( 'NONE', #120683, #2442 ) ;
#19956=ORIENTED_EDGE ( 'NONE', *, *, #100741, .F. ) ;
#19957=DIRECTION ( 'NONE',  ( 0.7071067811865487940, -0.7071067811865463515, 0.000000000000000000 ) ) ;
#19958=EDGE_CURVE ( 'NONE', #134932, #56792, #106365, .T. ) ;
#19959=ORIENTED_EDGE ( 'NONE', *, *, #54752, .F. ) ;
#19960=DIRECTION ( 'NONE',  ( 0.3543493200069162685, -0.000000000000000000, -0.9351131265310288487 ) ) ;
#19962=ORIENTED_EDGE ( 'NONE', *, *, #23476, .T. ) ;
#19964=PLANE ( 'NONE',  #14112 ) ;
#19965=VERTEX_POINT ( 'NONE', #128181 ) ;
#19966=DIRECTION ( 'NONE',  ( -0.3543493200069162685, -0.000000000000000000, -0.9351131265310288487 ) ) ;
#19967=DIRECTION ( 'NONE',  ( -0.000000000000000000, -0.000000000000000000, 1.000000000000000000 ) ) ;
#19968=DIRECTION ( 'NONE',  ( 0.7071067811865486830, -0.7071067811865464625, -0.000000000000000000 ) ) ;
#19969=EDGE_LOOP ( 'NONE', ( #121939, #120565, #100707, #36953, #18668 ) ) ;
#19970=ORIENTED_EDGE ( 'NONE', *, *, #2039, .T. ) ;
#19972=LINE ( 'NONE', #118578, #30598 ) ;
#19973=DIRECTION ( 'NONE',  ( 0.7071067811865487940, 0.7071067811865463515, 0.000000000000000000 ) ) ;
#19975=LINE ( 'NONE', #41750, #129615 ) ;
#19976=LINE ( 'NONE', #64223, #39110 ) ;
#19977=ORIENTED_EDGE ( 'NONE', *, *, #119747, .F. ) ;
#19978=DIRECTION ( 'NONE',  ( -0.6830127018922181881, 0.6830127018922202975, -0.2588190451025214056 ) ) ;
#19979=ADVANCED_FACE ( 'NONE', ( #138328 ), #52035, .T. ) ;
#19980=CARTESIAN_POINT ( 'NONE',  ( 27.18398860626900060, 28.73617430169806042, 5.000000000000000000 ) ) ;
#19982=VECTOR ( 'NONE', #88861, 1000.000000000000227 ) ;
#19983=ORIENTED_EDGE ( 'NONE', *, *, #87936, .T. ) ;
#19984=DIRECTION ( 'NONE',  ( -0.7071067811865486830, -0.7071067811865464625, 0.000000000000000000 ) ) ;
#19985=ORIENTED_EDGE ( 'NONE', *, *, #59368, .F. ) ;
#19988=DIRECTION ( 'NONE',  ( 0.7071067811865487940, 0.7071067811865463515, 0.000000000000000000 ) ) ;
#19989=VECTOR ( 'NONE', #135876, 1000.000000000000000 ) ;
#19990=CARTESIAN_POINT ( 'NONE',  ( 7.171830600776425868, 12.75929247661559529, 4.000000000000000000 ) ) ;
#19991=ORIENTED_EDGE ( 'NONE', *, *, #1078, .T. ) ;
#19992=DIRECTION ( 'NONE',  ( -0.7071067811865486830, 0.7071067811865464625, 0.000000000000000000 ) ) ;
#19993=CARTESIAN_POINT ( 'NONE',  ( 34.49999999999976552, 21.05432934483073026, 4.994342998332161443 ) ) ;
#19995=ADVANCED_FACE ( 'NONE', ( #38306 ), #49200, .F. ) ;
#19996=CARTESIAN_POINT ( 'NONE',  ( 24.75860074219779605, 21.72500000000000853, 5.000000000000000000 ) ) ;
#19997=CARTESIAN_POINT ( 'NONE',  ( 34.45011844616451668, -8.997695858405966973, 5.000000000000000888 ) ) ;
#19998=VERTEX_POINT ( 'NONE', #18658 ) ;
#20000=CARTESIAN_POINT ( 'NONE',  ( 0.000000000000000000, 0.000000000000000000, 5.000000000000000000 ) ) ;
#20001=DIRECTION ( 'NONE',  ( 0.7071067811865487940, 0.7071067811865463515, 0.000000000000000000 ) ) ;
#20002=CARTESIAN_POINT ( 'NONE',  ( -6.489213562373093325, -27.52281430457059841, 5.000000000000000000 ) ) ;
#20003=ORIENTED_EDGE ( 'NONE', *, *, #52298, .F. ) ;
#20004=VECTOR ( 'NONE', #138837, 999.9999999999998863 ) ;
#20005=ORIENTED_EDGE ( 'NONE', *, *, #33227, .F. ) ;
#20007=ORIENTED_EDGE ( 'NONE', *, *, #141487, .F. ) ;
#20008=DIRECTION ( 'NONE',  ( -0.6830127018922181881, 0.6830127018922202975, -0.2588190451025214056 ) ) ;
#20009=CARTESIAN_POINT ( 'NONE',  ( -7.069960254864042781, -0.7407075233842770334, 13.87443053587612418 ) ) ;
#20010=CARTESIAN_POINT ( 'NONE',  ( 15.48921356237309510, -27.52281430457066236, 5.000000000000000000 ) ) ;
#20011=CARTESIAN_POINT ( 'NONE',  ( -1.828169399223515512, 21.75929247661549581, 4.000000000000000000 ) ) ;
#20012=ORIENTED_EDGE ( 'NONE', *, *, #141990, .T. ) ;
#20013=CARTESIAN_POINT ( 'NONE',  ( 28.49999999999980815, -7.420205493532869845, -2.617629953481187766 ) ) ;
#20014=CARTESIAN_POINT ( 'NONE',  ( -15.32816939922341781, -15.74070752338412049, 4.000000000000000000 ) ) ;
#20015=VERTEX_POINT ( 'NONE', #29541 ) ;
#20016=EDGE_CURVE ( 'NONE', #80619, #102502, #117249, .T. ) ;
#20017=AXIS2_PLACEMENT_3D ( 'NONE', #69295, #46127, #79500 ) ;
#20018=CARTESIAN_POINT ( 'NONE',  ( 21.45983838949727129, 18.75929247661552068, 8.305906642995537936 ) ) ;
#20019=PLANE ( 'NONE',  #96583 ) ;
#20020=CARTESIAN_POINT ( 'NONE',  ( 54.48921356237310221, -27.52281430457093236, 5.000000000000000000 ) ) ;
#20021=VERTEX_POINT ( 'NONE', #84663 ) ;
#20022=ORIENTED_EDGE ( 'NONE', *, *, #96906, .T. ) ;
#20023=EDGE_CURVE ( 'NONE', #135612, #63645, #95517, .T. ) ;
#20024=VECTOR ( 'NONE', #77309, 1000.000000000000000 ) ;
#20025=CARTESIAN_POINT ( 'NONE',  ( 12.48921356237309155, -27.52281430457064104, 5.000000000000000000 ) ) ;
#20027=CARTESIAN_POINT ( 'NONE',  ( 34.92499999999998295, -14.24070752338413293, 4.255531930566171184 ) ) ;
#20029=DIRECTION ( 'NONE',  ( -0.7071067811865487940, 0.7071067811865463515, 0.000000000000000000 ) ) ;
#20030=CARTESIAN_POINT ( 'NONE',  ( -18.70701326429291456, -21.74070752338405654, 4.999753212805221558 ) ) ;
#20031=VECTOR ( 'NONE', #47723, 1000.000000000000000 ) ;
#20035=ORIENTED_EDGE ( 'NONE', *, *, #77447, .T. ) ;
#20036=VECTOR ( 'NONE', #1254, 1000.000000000000000 ) ;
#20037=VECTOR ( 'NONE', #81691, 1000.000000000000000 ) ;
#20040=VERTEX_POINT ( 'NONE', #16522 ) ;
#20044=DIRECTION ( 'NONE',  ( -4.681814790819591790E-17, -0.3543493200069152693, 0.9351131265310292928 ) ) ;
#20045=DIRECTION ( 'NONE',  ( -0.7071067811865487940, 0.7071067811865463515, 0.000000000000000000 ) ) ;
#20046=VERTEX_POINT ( 'NONE', #5636 ) ;
#20047=CARTESIAN_POINT ( 'NONE',  ( 15.32816939922342669, 14.25929247661556865, 4.000000000000000000 ) ) ;
#20048=DIRECTION ( 'NONE',  ( 0.7071067811865486830, -0.7071067811865464625, -0.000000000000000000 ) ) ;
#20049=DIRECTION ( 'NONE',  ( -0.6830127018922180770, -0.6830127018922204085, -0.2588190451025213501 ) ) ;
#20050=FACE_OUTER_BOUND ( 'NONE', #80990, .T. ) ;
#20051=DIRECTION ( 'NONE',  ( 0.7071067811865486830, -0.7071067811865464625, -0.000000000000000000 ) ) ;
#20052=CARTESIAN_POINT ( 'NONE',  ( 18.29974487139159223, -27.71228299555219010, 4.000000000000000000 ) ) ;
#20053=ORIENTED_EDGE ( 'NONE', *, *, #45032, .T. ) ;
#20055=LINE ( 'NONE', #8437, #125259 ) ;
#20056=ORIENTED_EDGE ( 'NONE', *, *, #127769, .F. ) ;
#20058=ORIENTED_EDGE ( 'NONE', *, *, #79142, .F. ) ;
#20059=ORIENTED_EDGE ( 'NONE', *, *, #141111, .F. ) ;
#20060=VERTEX_POINT ( 'NONE', #7784 ) ;
#20062=ORIENTED_EDGE ( 'NONE', *, *, #132851, .T. ) ;
#20063=VERTEX_POINT ( 'NONE', #137628 ) ;
#20064=DIRECTION ( 'NONE',  ( 0.7071067811865487940, 0.7071067811865463515, 0.000000000000000000 ) ) ;
#20065=EDGE_CURVE ( 'NONE', #80065, #90172, #94089, .T. ) ;
#20066=VECTOR ( 'NONE', #123185, 1000.000000000000000 ) ;
#20068=( BOUNDED_CURVE ( )  B_SPLINE_CURVE ( 3, ( #92409, #59137, #124347, #123663 ),
 .UNSPECIFIED., .F., .T. ) 
 B_SPLINE_CURVE_WITH_KNOTS ( ( 4, 4 ),
 ( 2.099584536334365925, 2.152415457235772767 ),
 .UNSPECIFIED. ) 
 CURVE ( )  GEOMETRIC_REPRESENTATION_ITEM ( )  RATIONAL_B_SPLINE_CURVE ( ( 1.000000000000000000, 0.9997674213408587196, 0.9997674213408587196, 1.000000000000000000 ) ) 
 REPRESENTATION_ITEM ( '' )  );
#20069=CARTESIAN_POINT ( 'NONE',  ( -5.999999999999956479, 12.83542986846996570, -1.025386466790356943 ) ) ;
#20070=ADVANCED_FACE ( 'NONE', ( #15775 ), #82521, .T. ) ;
#20071=LINE ( 'NONE', #75907, #62858 ) ;
#20072=ORIENTED_EDGE ( 'NONE', *, *, #112858, .T. ) ;
#20073=DIRECTION ( 'NONE',  ( -0.7071067811865486830, 0.7071067811865464625, 0.000000000000000000 ) ) ;
#20075=LINE ( 'NONE', #133167, #7605 ) ;
#20076=ADVANCED_FACE ( 'NONE', ( #126709 ), #27396, .F. ) ;
#20078=LINE ( 'NONE', #31694, #79264 ) ;
#20079=DIRECTION ( 'NONE',  ( 0.6830127018922180770, 0.6830127018922202975, -0.2588190451025213501 ) ) ;
#20080=ORIENTED_EDGE ( 'NONE', *, *, #33468, .T. ) ;
#20081=DIRECTION ( 'NONE',  ( 1.000000000000000000, 0.000000000000000000, 0.000000000000000000 ) ) ;
#20083=EDGE_LOOP ( 'NONE', ( #21368, #29209, #41960 ) ) ;
#20084=EDGE_LOOP ( 'NONE', ( #87176, #128799, #53750, #81221 ) ) ;
#20086=ORIENTED_EDGE ( 'NONE', *, *, #55881, .T. ) ;
#20087=CARTESIAN_POINT ( 'NONE',  ( -35.99451991528749772, 28.92564299267963079, 4.000000000000000000 ) ) ;
#20088=FACE_OUTER_BOUND ( 'NONE', #76548, .T. ) ;
#20089=EDGE_CURVE ( 'NONE', #116410, #115114, #17254, .T. ) ;
#20090=CARTESIAN_POINT ( 'NONE',  ( -14.99451991528749595, 28.92564299267948513, 4.000000000000000000 ) ) ;
#20094=ORIENTED_EDGE ( 'NONE', *, *, #27883, .T. ) ;
#20095=ADVANCED_FACE ( 'NONE', ( #65071 ), #119397, .F. ) ;
#20096=AXIS2_PLACEMENT_3D ( 'NONE', #11665, #70424, #137784 ) ;
#20098=CARTESIAN_POINT ( 'NONE',  ( 11.70025512860841133, -27.71228299555198049, 4.000000000000000000 ) ) ;
#20102=ORIENTED_EDGE ( 'NONE', *, *, #64266, .T. ) ;
#20103=ORIENTED_EDGE ( 'NONE', *, *, #18591, .F. ) ;
#20104=ORIENTED_EDGE ( 'NONE', *, *, #68236, .T. ) ;
#20105=CARTESIAN_POINT ( 'NONE',  ( -32.99999999999976552, -18.03360074219755660, 5.000000000000000000 ) ) ;
#20107=ADVANCED_FACE ( 'NONE', ( #87516 ), #141161, .F. ) ;
#20109=DIRECTION ( 'NONE',  ( 1.000000000000000000, 0.000000000000000000, 0.000000000000000000 ) ) ;
#20111=PLANE ( 'NONE',  #59932 ) ;
#20114=LINE ( 'NONE', #64360, #25766 ) ;
#20115=VERTEX_POINT ( 'NONE', #52726 ) ;
#20116=CARTESIAN_POINT ( 'NONE',  ( -26.54016161050243738, 18.75929247661552779, 8.305906642995426026 ) ) ;
#20117=EDGE_CURVE ( 'NONE', #136035, #29037, #120100, .T. ) ;
#20118=VERTEX_POINT ( 'NONE', #88237 ) ;
#20119=LINE ( 'NONE', #507, #8237 ) ;
#20120=ORIENTED_EDGE ( 'NONE', *, *, #4892, .T. ) ;
#20121=CARTESIAN_POINT ( 'NONE',  ( 22.88982677111772546, -22.22499999999999787, 4.785647885939350310 ) ) ;
#20122=FACE_OUTER_BOUND ( 'NONE', #92955, .T. ) ;
#20123=ORIENTED_EDGE ( 'NONE', *, *, #112509, .T. ) ;
#20124=VECTOR ( 'NONE', #51442, 1000.000000000000000 ) ;
#20125=LINE ( 'NONE', #33211, #19073 ) ;
#20126=EDGE_CURVE ( 'NONE', #44653, #60654, #73049, .T. ) ;
#20127=ORIENTED_EDGE ( 'NONE', *, *, #39901, .T. ) ;
#20128=LINE ( 'NONE', #516, #36912 ) ;
#20129=ORIENTED_EDGE ( 'NONE', *, *, #99935, .F. ) ;
#20130=CARTESIAN_POINT ( 'NONE',  ( -19.21071296386495675, 9.141836041257182188, 4.000000000000000000 ) ) ;
#20131=EDGE_LOOP ( 'NONE', ( #15149, #27108, #123065, #80900 ) ) ;
#20132=VECTOR ( 'NONE', #44523, 1000.000000000000000 ) ;
#20133=AXIS2_PLACEMENT_3D ( 'NONE', #100816, #121828, #21106 ) ;
#20134=VECTOR ( 'NONE', #80640, 1000.000000000000227 ) ;
#20135=ADVANCED_FACE ( 'NONE', ( #130323 ), #9185, .T. ) ;
#20138=DIRECTION ( 'NONE',  ( -0.000000000000000000, 0.000000000000000000, 1.000000000000000000 ) ) ;
#20139=CARTESIAN_POINT ( 'NONE',  ( 23.20710678118638626, 15.75929247661555443, 5.000000000000000000 ) ) ;
#20140=DIRECTION ( 'NONE',  ( 0.7071067811865487940, 0.7071067811865463515, 0.000000000000000000 ) ) ;
#20141=DIRECTION ( 'NONE',  ( -0.7071067811865486830, -0.7071067811865464625, 0.000000000000000000 ) ) ;
#20143=CARTESIAN_POINT ( 'NONE',  ( 22.49999999999984723, -4.912538124160710673, 4.000000000000000000 ) ) ;
#20146=VECTOR ( 'NONE', #117527, 1000.000000000000000 ) ;
#20147=DIRECTION ( 'NONE',  ( -0.000000000000000000, 0.3543493200069153248, 0.9351131265310292928 ) ) ;
#20148=LINE ( 'NONE', #131075, #87232 ) ;
#20150=VERTEX_POINT ( 'NONE', #64338 ) ;
#20151=DIRECTION ( 'NONE',  ( 0.7071067811865487940, 0.7071067811865463515, 0.000000000000000000 ) ) ;
#20152=VERTEX_POINT ( 'NONE', #33175 ) ;
#20154=ORIENTED_EDGE ( 'NONE', *, *, #33278, .T. ) ;
#20156=PLANE ( 'NONE',  #30276 ) ;
#20157=EDGE_CURVE ( 'NONE', #68874, #138697, #21544, .T. ) ;
#20159=CARTESIAN_POINT ( 'NONE',  ( 25.49999999999983302, -14.94781430457066840, 5.000000000000000000 ) ) ;
#20160=ORIENTED_EDGE ( 'NONE', *, *, #59867, .T. ) ;
#20161=DIRECTION ( 'NONE',  ( -0.000000000000000000, 0.000000000000000000, 1.000000000000000000 ) ) ;
#20162=VECTOR ( 'NONE', #119733, 1000.000000000000000 ) ;
#20163=LINE ( 'NONE', #31786, #114624 ) ;
#20164=CARTESIAN_POINT ( 'NONE',  ( 10.49999999999992539, -16.91253812416058722, 4.000000000000000000 ) ) ;
#20165=PLANE ( 'NONE',  #82679 ) ;
#20166=LINE ( 'NONE', #72483, #14473 ) ;
#20167=VERTEX_POINT ( 'NONE', #97668 ) ;
#20169=ORIENTED_EDGE ( 'NONE', *, *, #127353, .T. ) ;
#20172=ORIENTED_EDGE ( 'NONE', *, *, #20023, .F. ) ;
#20174=VECTOR ( 'NONE', #57862, 999.9999999999998863 ) ;
#20175=LINE ( 'NONE', #119485, #87105 ) ;
#20176=VERTEX_POINT ( 'NONE', #42610 ) ;
#20177=FACE_OUTER_BOUND ( 'NONE', #117338, .T. ) ;
#20178=CARTESIAN_POINT ( 'NONE',  ( 24.18398860626899705, 28.73617430169804265, 5.000000000000000000 ) ) ;
#20180=EDGE_LOOP ( 'NONE', ( #106856, #16890, #91685 ) ) ;
#20181=LINE ( 'NONE', #76021, #42003 ) ;
#20184=CARTESIAN_POINT ( 'NONE',  ( 12.18398860626900060, 28.73617430169795739, 5.000000000000000000 ) ) ;
#20185=DIRECTION ( 'NONE',  ( 1.000000000000000000, 0.000000000000000000, 0.000000000000000000 ) ) ;
#20186=ORIENTED_EDGE ( 'NONE', *, *, #8912, .T. ) ;
#20187=VERTEX_POINT ( 'NONE', #77384 ) ;
#20188=VECTOR ( 'NONE', #85304, 1000.000000000000000 ) ;
#20189=EDGE_CURVE ( 'NONE', #47526, #58114, #76667, .T. ) ;
#20190=ORIENTED_EDGE ( 'NONE', *, *, #47947, .T. ) ;
#20191=CARTESIAN_POINT ( 'NONE',  ( 28.35824297541122263, 15.75929247661555799, 19.34181609438693172 ) ) ;
#20192=EDGE_CURVE ( 'NONE', #100169, #142746, #142616, .T. ) ;
#20193=FACE_OUTER_BOUND ( 'NONE', #73958, .T. ) ;
#20196=CARTESIAN_POINT ( 'NONE',  ( -5.999999999999953815, -18.03360074219754949, 5.000000000000000000 ) ) ;
#20197=ORIENTED_EDGE ( 'NONE', *, *, #18787, .T. ) ;
#20198=VECTOR ( 'NONE', #13258, 1000.000000000000000 ) ;
#20199=VECTOR ( 'NONE', #26083, 1000.000000000000000 ) ;
#20201=ORIENTED_EDGE ( 'NONE', *, *, #83780, .T. ) ;
#20202=CARTESIAN_POINT ( 'NONE',  ( -63.48921356237309510, -27.52281430457099631, 5.000000000000000000 ) ) ;
#20204=ORIENTED_EDGE ( 'NONE', *, *, #25985, .F. ) ;
#20205=ADVANCED_FACE ( 'NONE', ( #86809 ), #131027, .F. ) ;
#20206=CARTESIAN_POINT ( 'NONE',  ( 27.29974487139158512, -27.71228299555225405, 4.000000000000000000 ) ) ;
#20207=CARTESIAN_POINT ( 'NONE',  ( 34.92499999999998295, 22.22500000000000142, 4.500000000000000888 ) ) ;
#20210=LINE ( 'NONE', #19521, #6689 ) ;
#20211=DIRECTION ( 'NONE',  ( 0.6830127018922180770, -0.6830127018922204085, -0.2588190451025213501 ) ) ;
#20212=LINE ( 'NONE', #84108, #53026 ) ;
#20214=ADVANCED_FACE ( 'NONE', ( #98396 ), #10636, .F. ) ;
#20215=FACE_OUTER_BOUND ( 'NONE', #44590, .T. ) ;
#20216=ORIENTED_EDGE ( 'NONE', *, *, #133433, .F. ) ;
#20217=CARTESIAN_POINT ( 'NONE',  ( -9.706123077391888287, 22.22500000000000142, 4.000000000000000000 ) ) ;
#20219=ORIENTED_EDGE ( 'NONE', *, *, #10006, .F. ) ;
#20220=PLANE ( 'NONE',  #80578 ) ;
#20223=CARTESIAN_POINT ( 'NONE',  ( -8.700255128608413102, -27.71228299555199825, 4.000000000000000000 ) ) ;
#20225=CARTESIAN_POINT ( 'NONE',  ( 14.99999999999989519, 14.87792677143810316, -11.06722581663436777 ) ) ;
#20226=ORIENTED_EDGE ( 'NONE', *, *, #364, .T. ) ;
#20227=ORIENTED_EDGE ( 'NONE', *, *, #13494, .F. ) ;
#20228=VECTOR ( 'NONE', #54342, 1000.000000000000000 ) ;
#20230=AXIS2_PLACEMENT_3D ( 'NONE', #86585, #119181, #42373 ) ;
#20231=VECTOR ( 'NONE', #78489, 999.9999999999998863 ) ;
#20232=VECTOR ( 'NONE', #129133, 1000.000000000000000 ) ;
#20234=CARTESIAN_POINT ( 'NONE',  ( 0.000000000000000000, 0.000000000000000000, 5.000000000000000000 ) ) ;
#20235=DIRECTION ( 'NONE',  ( 0.7071067811865486830, -0.7071067811865464625, -0.000000000000000000 ) ) ;
#20236=CARTESIAN_POINT ( 'NONE',  ( -12.18398860626900060, 28.73617430169795739, 5.000000000000000000 ) ) ;
#20238=CARTESIAN_POINT ( 'NONE',  ( -22.17183060077631396, 21.75929247661548871, 4.000000000000000000 ) ) ;
#20239=EDGE_CURVE ( 'NONE', #121929, #10073, #74519, .T. ) ;
#20240=LINE ( 'NONE', #77533, #140834 ) ;
#20241=DIRECTION ( 'NONE',  ( 0.6830127018922181881, 0.6830127018922202975, -0.2588190451025214056 ) ) ;
#20242=VECTOR ( 'NONE', #117870, 1000.000000000000000 ) ;
#20243=CARTESIAN_POINT ( 'NONE',  ( 34.53569095963128177, 22.21392809009763170, 4.239552123775266246 ) ) ;
#20245=EDGE_CURVE ( 'NONE', #70018, #98898, #78790, .T. ) ;
#20246=CARTESIAN_POINT ( 'NONE',  ( -27.29974487139158512, -27.71228299555225405, 4.000000000000000000 ) ) ;
#20247=FACE_OUTER_BOUND ( 'NONE', #114675, .T. ) ;
#20248=DIRECTION ( 'NONE',  ( -0.7071067811865486830, -0.7071067811865464625, 0.000000000000000000 ) ) ;
#20250=EDGE_LOOP ( 'NONE', ( #91747, #71998, #20484, #93898 ) ) ;
#20251=ORIENTED_EDGE ( 'NONE', *, *, #128910, .F. ) ;
#20252=ORIENTED_EDGE ( 'NONE', *, *, #116490, .F. ) ;
#20253=DIRECTION ( 'NONE',  ( 0.7071067811865487940, 0.7071067811865463515, -0.000000000000000000 ) ) ;
#20254=ORIENTED_EDGE ( 'NONE', *, *, #31858, .T. ) ;
#20255=EDGE_CURVE ( 'NONE', #36664, #121857, #1872, .T. ) ;
#20256=ORIENTED_EDGE ( 'NONE', *, *, #56479, .F. ) ;
#20257=DIRECTION ( 'NONE',  ( 0.7071067811865486830, -0.7071067811865464625, -0.000000000000000000 ) ) ;
#20258=CARTESIAN_POINT ( 'NONE',  ( -20.99999999999984723, 11.96639925780213609, 5.000000000000000000 ) ) ;
#20259=EDGE_CURVE ( 'NONE', #32784, #60759, #89648, .T. ) ;
#20260=EDGE_CURVE ( 'NONE', #106881, #99164, #100540, .T. ) ;
#20261=DIRECTION ( 'NONE',  ( -0.7071067811865487940, 0.7071067811865463515, -0.000000000000000000 ) ) ;
#20262=EDGE_LOOP ( 'NONE', ( #12774, #134651, #68506, #82454 ) ) ;
#20263=VECTOR ( 'NONE', #62738, 1000.000000000000000 ) ;
#20264=LINE ( 'NONE', #52884, #134462 ) ;
#20265=ORIENTED_EDGE ( 'NONE', *, *, #85066, .F. ) ;
#20266=LINE ( 'NONE', #132663, #69942 ) ;
#20267=LINE ( 'NONE', #64509, #58936 ) ;
#20268=ADVANCED_FACE ( 'NONE', ( #58513 ), #123004, .F. ) ;
#20270=ORIENTED_EDGE ( 'NONE', *, *, #137451, .F. ) ;
#20272=ADVANCED_FACE ( 'NONE', ( #125127 ), #25820, .F. ) ;
#20274=DIRECTION ( 'NONE',  ( 0.7071067811865487940, 0.7071067811865463515, 0.000000000000000000 ) ) ;
#20275=DIRECTION ( 'NONE',  ( 0.7071067811865487940, 0.7071067811865463515, 0.000000000000000000 ) ) ;
#20277=ORIENTED_EDGE ( 'NONE', *, *, #115615, .F. ) ;
#20278=CARTESIAN_POINT ( 'NONE',  ( 23.99999999999982592, 11.58746187583913390, 4.000000000000000000 ) ) ;
#20279=ORIENTED_EDGE ( 'NONE', *, *, #39665, .T. ) ;
#20280=CARTESIAN_POINT ( 'NONE',  ( 72.29974487139158157, -27.71228299555256669, 4.000000000000000000 ) ) ;
#20281=LINE ( 'NONE', #50796, #16343 ) ;
#20282=EDGE_CURVE ( 'NONE', #48369, #113729, #102688, .T. ) ;
#20283=CARTESIAN_POINT ( 'NONE',  ( 51.48921356237309510, -27.52281430457091460, 5.000000000000000000 ) ) ;
#20284=DIRECTION ( 'NONE',  ( 0.3543493200069162685, -0.000000000000000000, -0.9351131265310288487 ) ) ;
#20285=EDGE_LOOP ( 'NONE', ( #60216, #140157, #51340, #139141 ) ) ;
#20286=CARTESIAN_POINT ( 'NONE',  ( -15.29974487139158867, -27.71228299555216879, 4.000000000000000000 ) ) ;
#20287=CARTESIAN_POINT ( 'NONE',  ( -18.48921356237309510, -27.52281430457068367, 5.000000000000000000 ) ) ;
#20288=FACE_OUTER_BOUND ( 'NONE', #110438, .T. ) ;
#20289=EDGE_LOOP ( 'NONE', ( #23084, #48301, #45252, #98899 ) ) ;
#20292=DIRECTION ( 'NONE',  ( 0.7071067811865487940, -0.7071067811865463515, 0.000000000000000000 ) ) ;
#20294=LINE ( 'NONE', #10146, #85726 ) ;
#20295=ORIENTED_EDGE ( 'NONE', *, *, #106437, .F. ) ;
#20296=ORIENTED_EDGE ( 'NONE', *, *, #108090, .T. ) ;
#20298=LINE ( 'NONE', #131226, #11318 ) ;
#20299=EDGE_CURVE ( 'NONE', #82496, #6537, #136008, .T. ) ;
#20300=ORIENTED_EDGE ( 'NONE', *, *, #27127, .T. ) ;
#20302=EDGE_CURVE ( 'NONE', #24994, #6521, #14931, .T. ) ;
#20303=FACE_OUTER_BOUND ( 'NONE', #116482, .T. ) ;
#20304=ADVANCED_FACE ( 'NONE', ( #33863 ), #69346, .F. ) ;
#20305=DIRECTION ( 'NONE',  ( 0.000000000000000000, -1.000000000000000000, 0.000000000000000000 ) ) ;
#20307=CARTESIAN_POINT ( 'NONE',  ( -20.67183060077632106, -6.740707523384212863, 4.000000000000000000 ) ) ;
#20308=DIRECTION ( 'NONE',  ( 0.7071067811865486830, -0.7071067811865464625, -0.000000000000000000 ) ) ;
#20309=CARTESIAN_POINT ( 'NONE',  ( -33.48921356237309510, -27.52281430457078670, 5.000000000000000000 ) ) ;
#20310=DIRECTION ( 'NONE',  ( 0.7071067811865487940, 0.7071067811865463515, -0.000000000000000000 ) ) ;
#20311=PLANE ( 'NONE',  #92962 ) ;
#20313=EDGE_CURVE ( 'NONE', #117224, #104204, #103358, .T. ) ;
#20314=DIRECTION ( 'NONE',  ( -0.000000000000000000, -0.3543493200069152693, 0.9351131265310292928 ) ) ;
#20315=FACE_OUTER_BOUND ( 'NONE', #14944, .T. ) ;
#20316=ORIENTED_EDGE ( 'NONE', *, *, #58492, .F. ) ;
#20317=VERTEX_POINT ( 'NONE', #46187 ) ;
#20318=ORIENTED_EDGE ( 'NONE', *, *, #37705, .F. ) ;
#20320=VECTOR ( 'NONE', #79249, 1000.000000000000000 ) ;
#20322=ORIENTED_EDGE ( 'NONE', *, *, #31460, .F. ) ;
#20323=ORIENTED_EDGE ( 'NONE', *, *, #83411, .T. ) ;
#20324=LINE ( 'NONE', #140011, #121910 ) ;
#20325=DIRECTION ( 'NONE',  ( 0.6830127018922180770, -0.6830127018922204085, -0.2588190451025213501 ) ) ;
#20326=ORIENTED_EDGE ( 'NONE', *, *, #16731, .F. ) ;
#20327=AXIS2_PLACEMENT_3D ( 'NONE', #48274, #61347, #136705 ) ;
#20330=VECTOR ( 'NONE', #87994, 1000.000000000000227 ) ;
#20331=CARTESIAN_POINT ( 'NONE',  ( -7.499999999999947597, -5.568876922607761237, 4.000000000000000000 ) ) ;
#20332=FACE_OUTER_BOUND ( 'NONE', #7406, .T. ) ;
#20334=VERTEX_POINT ( 'NONE', #48287 ) ;
#20335=CARTESIAN_POINT ( 'NONE',  ( -36.18398860626899705, 28.73617430169812437, 5.000000000000000000 ) ) ;
#20336=DIRECTION ( 'NONE',  ( -0.6830127018922180770, -0.6830127018922204085, -0.2588190451025213501 ) ) ;
#20337=VECTOR ( 'NONE', #137956, 1000.000000000000000 ) ;
#20338=DIRECTION ( 'NONE',  ( -0.000000000000000000, -0.3543493200069152693, 0.9351131265310292928 ) ) ;
#20344=VERTEX_POINT ( 'NONE', #78081 ) ;
#20345=VERTEX_POINT ( 'NONE', #57770 ) ;
#20347=ORIENTED_EDGE ( 'NONE', *, *, #3928, .F. ) ;
#20349=EDGE_CURVE ( 'NONE', #13343, #59700, #122256, .T. ) ;
#20350=CARTESIAN_POINT ( 'NONE',  ( -34.92500000000001137, 22.22500000000000142, 4.500000000000000888 ) ) ;
#20353=CARTESIAN_POINT ( 'NONE',  ( 24.29974487139158867, -27.71228299555223273, 4.000000000000000000 ) ) ;
#20354=DIRECTION ( 'NONE',  ( -0.7071067811865486830, -0.7071067811865464625, -0.000000000000000000 ) ) ;
#20356=ORIENTED_EDGE ( 'NONE', *, *, #124443, .T. ) ;
#20357=ORIENTED_EDGE ( 'NONE', *, *, #69861, .F. ) ;
#20358=CARTESIAN_POINT ( 'NONE',  ( 50.99451991528749062, 28.92564299267973738, 4.000000000000000000 ) ) ;
#20359=LINE ( 'NONE', #130602, #117201 ) ;
#20363=EDGE_CURVE ( 'NONE', #8673, #26139, #45466, .T. ) ;
#20365=ORIENTED_EDGE ( 'NONE', *, *, #43242, .F. ) ;
#20367=EDGE_CURVE ( 'NONE', #49145, #30768, #12076, .T. ) ;
#20368=ORIENTED_EDGE ( 'NONE', *, *, #94592, .T. ) ;
#20369=DIRECTION ( 'NONE',  ( 0.6830127018922180770, -0.6830127018922204085, -0.2588190451025213501 ) ) ;
#20370=LINE ( 'NONE', #18966, #90221 ) ;
#20371=FACE_OUTER_BOUND ( 'NONE', #90766, .T. ) ;
#20372=VECTOR ( 'NONE', #83027, 1000.000000000000000 ) ;
#20373=LINE ( 'NONE', #21824, #9002 ) ;
#20374=ADVANCED_FACE ( 'NONE', ( #56361 ), #133876, .F. ) ;
#20375=EDGE_CURVE ( 'NONE', #17766, #3015, #2623, .T. ) ;
#20377=VERTEX_POINT ( 'NONE', #106944 ) ;
#20378=EDGE_CURVE ( 'NONE', #110736, #26697, #72238, .T. ) ;
#20379=CARTESIAN_POINT ( 'NONE',  ( 2.510786437626908008, -27.52281430457053446, 5.000000000000000000 ) ) ;
#20380=ORIENTED_EDGE ( 'NONE', *, *, #56667, .T. ) ;
#20381=ORIENTED_EDGE ( 'NONE', *, *, #14629, .F. ) ;
#20382=ORIENTED_EDGE ( 'NONE', *, *, #66737, .T. ) ;
#20383=EDGE_CURVE ( 'NONE', #2653, #20040, #116406, .T. ) ;
#20384=CARTESIAN_POINT ( 'NONE',  ( -36.48921356237310221, -27.52281430457080802, 5.000000000000000000 ) ) ;
#20385=ORIENTED_EDGE ( 'NONE', *, *, #8457, .T. ) ;
#20386=DIRECTION ( 'NONE',  ( 0.7071067811865487940, -0.7071067811865463515, 0.000000000000000000 ) ) ;
#20387=CARTESIAN_POINT ( 'NONE',  ( -14.29298673570684919, -21.74070752338405299, 4.999753212805220670 ) ) ;
#20388=LINE ( 'NONE', #103998, #36684 ) ;
#20389=EDGE_CURVE ( 'NONE', #98744, #133141, #83813, .T. ) ;
#20390=DIRECTION ( 'NONE',  ( -0.6830127018922181881, 0.6830127018922202975, -0.2588190451025214056 ) ) ;
#20391=FACE_BOUND ( 'NONE', #97604, .T. ) ;
#20392=VERTEX_POINT ( 'NONE', #51158 ) ;
#20394=LINE ( 'NONE', #64642, #431 ) ;
#20395=DIRECTION ( 'NONE',  ( 0.7071067811865487940, 0.7071067811865463515, -0.000000000000000000 ) ) ;
#20397=CARTESIAN_POINT ( 'NONE',  ( -13.49999999999988987, 19.46639925780206326, 5.000000000000000000 ) ) ;
#20398=ORIENTED_EDGE ( 'NONE', *, *, #9364, .T. ) ;
#20399=EDGE_CURVE ( 'NONE', #125435, #30701, #26540, .T. ) ;
#20400=VERTEX_POINT ( 'NONE', #38847 ) ;
#20402=LINE ( 'NONE', #107431, #5409 ) ;
#20403=ORIENTED_EDGE ( 'NONE', *, *, #127332, .T. ) ;
#20405=EDGE_LOOP ( 'NONE', ( #119023, #141331, #94218, #17127 ) ) ;
#20406=VECTOR ( 'NONE', #19013, 1000.000000000000000 ) ;
#20407=LINE ( 'NONE', #8098, #2435 ) ;
#20408=ORIENTED_EDGE ( 'NONE', *, *, #2345, .T. ) ;
#20409=DIRECTION ( 'NONE',  ( 0.7071067811865486830, -0.7071067811865464625, -0.000000000000000000 ) ) ;
#20410=EDGE_CURVE ( 'NONE', #53550, #55005, #105503, .T. ) ;
#20411=VERTEX_POINT ( 'NONE', #28702 ) ;
#20412=CARTESIAN_POINT ( 'NONE',  ( -29.99999999999978684, -9.412538124160658271, 4.000000000000000000 ) ) ;
#20414=EDGE_CURVE ( 'NONE', #98313, #62440, #38146, .T. ) ;
#20415=FACE_OUTER_BOUND ( 'NONE', #38271, .T. ) ;
#20416=DIRECTION ( 'NONE',  ( 0.7071067811865487940, -0.7071067811865463515, 0.000000000000000000 ) ) ;
#20417=CARTESIAN_POINT ( 'NONE',  ( 9.707106781186483957, 11.25929247661560417, 5.000000000000000000 ) ) ;
#20418=EDGE_CURVE ( 'NONE', #103755, #122205, #125871, .T. ) ;
#20420=DIRECTION ( 'NONE',  ( 1.000000000000000000, 0.000000000000000000, 0.000000000000000000 ) ) ;
#20421=VERTEX_POINT ( 'NONE', #106205 ) ;
#20422=ORIENTED_EDGE ( 'NONE', *, *, #75495, .T. ) ;
#20423=ORIENTED_EDGE ( 'NONE', *, *, #107742, .T. ) ;
#20425=VECTOR ( 'NONE', #131693, 1000.000000000000227 ) ;
#20426=VECTOR ( 'NONE', #33360, 1000.000000000000000 ) ;
#20427=DIRECTION ( 'NONE',  ( 0.7071067811865487940, 0.7071067811865463515, 0.000000000000000000 ) ) ;
#20428=VERTEX_POINT ( 'NONE', #59894 ) ;
#20429=EDGE_CURVE ( 'NONE', #135404, #27690, #27234, .T. ) ;
#20430=VECTOR ( 'NONE', #75518, 1000.000000000000000 ) ;
#20431=VERTEX_POINT ( 'NONE', #50445 ) ;
#20433=CARTESIAN_POINT ( 'NONE',  ( 23.99451991528749062, 28.92564299267954908, 4.000000000000000000 ) ) ;
#20434=PLANE ( 'NONE',  #57943 ) ;
#20436=DIRECTION ( 'NONE',  ( -0.6830127018922180770, -0.6830127018922204085, -0.2588190451025213501 ) ) ;
#20437=CIRCLE ( 'NONE', #101482, 5.968999999999998529 ) ;
#20439=DIRECTION ( 'NONE',  ( -0.7071067811865486830, -0.7071067811865464625, -0.000000000000000000 ) ) ;
#20441=LINE ( 'NONE', #120445, #103977 ) ;
#20442=VERTEX_POINT ( 'NONE', #137453 ) ;
#20444=EDGE_CURVE ( 'NONE', #55587, #100624, #94630, .T. ) ;
#20445=CARTESIAN_POINT ( 'NONE',  ( -2.816011393730999401, 28.73617430169785436, 5.000000000000000000 ) ) ;
#20446=DIRECTION ( 'NONE',  ( -0.000000000000000000, 0.3543493200069153248, 0.9351131265310292928 ) ) ;
#20447=CARTESIAN_POINT ( 'NONE',  ( -2.207106781186518596, -8.240707523384196875, 5.000000000000000000 ) ) ;
#20448=ORIENTED_EDGE ( 'NONE', *, *, #21739, .T. ) ;
#20449=VECTOR ( 'NONE', #131406, 1000.000000000000227 ) ;
#20451=ORIENTED_EDGE ( 'NONE', *, *, #20255, .F. ) ;
#20452=CARTESIAN_POINT ( 'NONE',  ( 28.49999999999980460, 1.466399257802250222, 5.000000000000000000 ) ) ;
#20453=EDGE_CURVE ( 'NONE', #59176, #35299, #104809, .T. ) ;
#20455=ORIENTED_EDGE ( 'NONE', *, *, #114654, .F. ) ;
#20456=VECTOR ( 'NONE', #64380, 1000.000000000000000 ) ;
#20457=LINE ( 'NONE', #64707, #90504 ) ;
#20458=DIRECTION ( 'NONE',  ( -0.3543493200069162685, -0.000000000000000000, -0.9351131265310288487 ) ) ;
#20459=VERTEX_POINT ( 'NONE', #115645 ) ;
#20460=VECTOR ( 'NONE', #71006, 1000.000000000000000 ) ;
#20461=DIRECTION ( 'NONE',  ( -0.6830127018922181881, 0.6830127018922202975, -0.2588190451025214056 ) ) ;
#20462=DIRECTION ( 'NONE',  ( 0.7071067811865486830, -0.7071067811865464625, -0.000000000000000000 ) ) ;
#20463=VECTOR ( 'NONE', #111979, 1000.000000000000114 ) ;
#20464=ORIENTED_EDGE ( 'NONE', *, *, #32071, .F. ) ;
#20465=VECTOR ( 'NONE', #42042, 1000.000000000000227 ) ;
#20467=DIRECTION ( 'NONE',  ( 0.7071067811865487940, 0.7071067811865463515, 0.000000000000000000 ) ) ;
#20468=VERTEX_POINT ( 'NONE', #49026 ) ;
#20469=ORIENTED_EDGE ( 'NONE', *, *, #4660, .T. ) ;
#20472=DIRECTION ( 'NONE',  ( -1.000000000000000000, 0.000000000000000000, 0.000000000000000000 ) ) ;
#20473=EDGE_CURVE ( 'NONE', #118275, #6107, #82364, .T. ) ;
#20474=DIRECTION ( 'NONE',  ( 0.7071067811865487940, 0.7071067811865463515, 0.000000000000000000 ) ) ;
#20476=VERTEX_POINT ( 'NONE', #71480 ) ;
#20478=LINE ( 'NONE', #108907, #86108 ) ;
#20479=DIRECTION ( 'NONE',  ( 0.7071067811865487940, 0.7071067811865463515, -0.000000000000000000 ) ) ;
#20480=AXIS2_PLACEMENT_3D ( 'NONE', #123167, #70246, #57212 ) ;
#20482=LINE ( 'NONE', #29235, #16304 ) ;
#20483=AXIS2_PLACEMENT_3D ( 'NONE', #135701, #80616, #15303 ) ;
#20484=ORIENTED_EDGE ( 'NONE', *, *, #15981, .F. ) ;
#20485=ORIENTED_EDGE ( 'NONE', *, *, #69966, .F. ) ;
#20486=CARTESIAN_POINT ( 'NONE',  ( 5.510786437626906675, -27.52281430457051314, 5.000000000000000000 ) ) ;
#20487=EDGE_LOOP ( 'NONE', ( #44205, #95094, #19273, #8040 ) ) ;
#20488=VERTEX_POINT ( 'NONE', #17772 ) ;
#20489=DIRECTION ( 'NONE',  ( 0.6830127018922180770, -0.6830127018922204085, -0.2588190451025213501 ) ) ;
#20490=ORIENTED_EDGE ( 'NONE', *, *, #98378, .F. ) ;
#20492=CARTESIAN_POINT ( 'NONE',  ( -16.49999999999988631, 18.43112307739199451, 4.000000000000000000 ) ) ;
#20493=CARTESIAN_POINT ( 'NONE',  ( -33.70612307739173019, 22.22500000000000142, 4.000000000000000000 ) ) ;
#20494=LINE ( 'NONE', #108929, #118175 ) ;
#20497=CARTESIAN_POINT ( 'NONE',  ( 4.499999999999966249, -20.53675388469230256, 2.352720554255903540 ) ) ;
#20498=PLANE ( 'NONE',  #127878 ) ;
#20499=DIRECTION ( 'NONE',  ( 1.000000000000000000, 0.000000000000000000, 0.000000000000000000 ) ) ;
#20501=FACE_OUTER_BOUND ( 'NONE', #5902, .T. ) ;
#20502=CARTESIAN_POINT ( 'NONE',  ( -18.18398860626898994, 28.73617430169800002, 5.000000000000000000 ) ) ;
#20507=VERTEX_POINT ( 'NONE', #6880 ) ;
#20509=DIRECTION ( 'NONE',  ( 1.000000000000000000, 0.000000000000000000, 0.000000000000000000 ) ) ;
#20510=CARTESIAN_POINT ( 'NONE',  ( -21.18398860626899349, 28.73617430169802134, 5.000000000000000000 ) ) ;
#20511=DIRECTION ( 'NONE',  ( -0.7071067811865487940, 0.7071067811865463515, -0.000000000000000000 ) ) ;
#20512=VERTEX_POINT ( 'NONE', #139621 ) ;
#20514=CARTESIAN_POINT ( 'NONE',  ( 8.999999999999932498, -11.35517001088071787, -1.126524801160087241 ) ) ;
#20515=CARTESIAN_POINT ( 'NONE',  ( -18.51665438641032679, 22.22500000000000142, 4.500000000000000888 ) ) ;
#20518=EDGE_CURVE ( 'NONE', #35500, #46353, #40302, .T. ) ;
#20519=ADVANCED_FACE ( 'NONE', ( #5469 ), #29377, .F. ) ;
#20520=CARTESIAN_POINT ( 'NONE',  ( 15.68879807097514956, -1.757674993583058898, 4.000000000000000000 ) ) ;
#20521=ORIENTED_EDGE ( 'NONE', *, *, #100711, .T. ) ;
#20523=FACE_OUTER_BOUND ( 'NONE', #77765, .T. ) ;
#20524=AXIS2_PLACEMENT_3D ( 'NONE', #38316, #18665, #62941 ) ;
#20525=VECTOR ( 'NONE', #38432, 1000.000000000000000 ) ;
#20526=DIRECTION ( 'NONE',  ( -0.7071067811865486830, 0.7071067811865464625, 0.000000000000000000 ) ) ;
#20530=VERTEX_POINT ( 'NONE', #42446 ) ;
#20532=ADVANCED_FACE ( 'NONE', ( #107655 ), #98915, .F. ) ;
#20533=EDGE_CURVE ( 'NONE', #10965, #86617, #22069, .T. ) ;
#20535=VERTEX_POINT ( 'NONE', #141748 ) ;
#20538=DIRECTION ( 'NONE',  ( -0.6830127018922181881, 0.6830127018922202975, -0.2588190451025214056 ) ) ;
#20539=DIRECTION ( 'NONE',  ( 0.7071067811865487940, -0.7071067811865463515, 0.000000000000000000 ) ) ;
#20541=DIRECTION ( 'NONE',  ( 0.6830127018922180770, -0.6830127018922204085, -0.2588190451025213501 ) ) ;
#20542=LINE ( 'NONE', #41599, #92549 ) ;
#20543=AXIS2_PLACEMENT_3D ( 'NONE', #69934, #134447, #80086 ) ;
#20544=EDGE_CURVE ( 'NONE', #40999, #106934, #94174, .T. ) ;
#20546=ORIENTED_EDGE ( 'NONE', *, *, #56137, .F. ) ;
#20549=EDGE_CURVE ( 'NONE', #28258, #75489, #11166, .T. ) ;
#20550=CARTESIAN_POINT ( 'NONE',  ( -6.005480084712508493, 28.92564299267933947, 4.000000000000000000 ) ) ;
#20551=CARTESIAN_POINT ( 'NONE',  ( -39.48921356237310221, -27.52281430457082934, 5.000000000000000000 ) ) ;
#20552=ORIENTED_EDGE ( 'NONE', *, *, #12926, .T. ) ;
#20553=ORIENTED_EDGE ( 'NONE', *, *, #79910, .T. ) ;
#20554=VECTOR ( 'NONE', #122472, 1000.000000000000000 ) ;
#20555=EDGE_CURVE ( 'NONE', #31876, #60798, #65642, .T. ) ;
#20557=LINE ( 'NONE', #64813, #70055 ) ;
#20558=EDGE_LOOP ( 'NONE', ( #52405, #95987, #46902, #57347 ) ) ;
#20560=ORIENTED_EDGE ( 'NONE', *, *, #96696, .F. ) ;
#20561=VECTOR ( 'NONE', #9066, 1000.000000000000000 ) ;
#20562=CARTESIAN_POINT ( 'NONE',  ( 31.82816939922330945, -8.240707523384191546, 4.000000000000000000 ) ) ;
#20564=DIRECTION ( 'NONE',  ( -0.7071067811865486830, -0.7071067811865464625, 0.000000000000000000 ) ) ;
#20566=VECTOR ( 'NONE', #132712, 1000.000000000000000 ) ;
#20567=VECTOR ( 'NONE', #127347, 1000.000000000000000 ) ;
#20568=AXIS2_PLACEMENT_3D ( 'NONE', #11366, #23713, #12817 ) ;
#20569=EDGE_CURVE ( 'NONE', #48401, #9427, #40988, .T. ) ;
#20570=CARTESIAN_POINT ( 'NONE',  ( 39.48921356237310221, -27.52281430457082934, 5.000000000000000000 ) ) ;
#20571=VECTOR ( 'NONE', #97690, 1000.000000000000000 ) ;
#20572=FACE_BOUND ( 'NONE', #60605, .T. ) ;
#20573=LINE ( 'NONE', #85129, #121928 ) ;
#20574=DIRECTION ( 'NONE',  ( -1.000000000000000000, 2.310445909535201824E-14, 0.000000000000000000 ) ) ;
#20576=DIRECTION ( 'NONE',  ( 0.7071067811865486830, -0.7071067811865464625, -0.000000000000000000 ) ) ;
#20577=EDGE_LOOP ( 'NONE', ( #89543, #29638, #135775, #99379 ) ) ;
#20579=VECTOR ( 'NONE', #59878, 1000.000000000000227 ) ;
#20580=DIRECTION ( 'NONE',  ( -0.7071067811865486830, -0.7071067811865464625, -0.000000000000000000 ) ) ;
#20582=VERTEX_POINT ( 'NONE', #108337 ) ;
#20583=EDGE_LOOP ( 'NONE', ( #92176, #135819, #5486, #35988 ) ) ;
#20585=ORIENTED_EDGE ( 'NONE', *, *, #9944, .F. ) ;
#20586=CARTESIAN_POINT ( 'NONE',  ( -48.48921356237309510, -27.52281430457089328, 5.000000000000000000 ) ) ;
#20587=EDGE_CURVE ( 'NONE', #138203, #137069, #121388, .T. ) ;
#20588=ORIENTED_EDGE ( 'NONE', *, *, #77123, .T. ) ;
#20589=LINE ( 'NONE', #8266, #99962 ) ;
#20591=LINE ( 'NONE', #108288, #5441 ) ;
#20592=EDGE_CURVE ( 'NONE', #90110, #32128, #129408, .T. ) ;
#20593=DIRECTION ( 'NONE',  ( 1.000000000000000000, 0.000000000000000000, 0.000000000000000000 ) ) ;
#20594=CARTESIAN_POINT ( 'NONE',  ( -18.48921356237309510, -27.52281430457068367, 5.000000000000000000 ) ) ;
#20595=DIRECTION ( 'NONE',  ( -0.000000000000000000, 0.3543493200069153248, 0.9351131265310292928 ) ) ;
#20597=DIRECTION ( 'NONE',  ( 0.7071067811865486830, -0.7071067811865464625, -0.000000000000000000 ) ) ;
#20598=CARTESIAN_POINT ( 'NONE',  ( -74.99451991528749772, 28.92564299267990435, 4.000000000000000000 ) ) ;
#20599=VERTEX_POINT ( 'NONE', #85185 ) ;
#20601=ORIENTED_EDGE ( 'NONE', *, *, #33616, .T. ) ;
#20602=DIRECTION ( 'NONE',  ( -0.6830127018922180770, -0.6830127018922204085, -0.2588190451025213501 ) ) ;
#20603=EDGE_CURVE ( 'NONE', #130004, #1441, #20643, .T. ) ;
#20604=CARTESIAN_POINT ( 'NONE',  ( -3.299744871391591339, -27.71228299555208352, 4.000000000000000000 ) ) ;
#20606=ORIENTED_EDGE ( 'NONE', *, *, #71520, .T. ) ;
#20607=EDGE_LOOP ( 'NONE', ( #30855, #95117, #128674, #48057 ) ) ;
#20612=ADVANCED_FACE ( 'NONE', ( #64897 ), #140299, .F. ) ;
#20613=LINE ( 'NONE', #77188, #123434 ) ;
#20616=VERTEX_POINT ( 'NONE', #98231 ) ;
#20617=EDGE_CURVE ( 'NONE', #42725, #55653, #142455, .T. ) ;
#20618=DIRECTION ( 'NONE',  ( 0.7071067811865487940, 0.7071067811865463515, 0.000000000000000000 ) ) ;
#20619=EDGE_LOOP ( 'NONE', ( #24510, #60680, #80621, #105849 ) ) ;
#20621=CARTESIAN_POINT ( 'NONE',  ( -21.48921356237309155, -27.52281430457070499, 5.000000000000000000 ) ) ;
#20622=DIRECTION ( 'NONE',  ( -0.000000000000000000, -0.3543493200069152693, 0.9351131265310292928 ) ) ;
#20623=ORIENTED_EDGE ( 'NONE', *, *, #125511, .F. ) ;
#20624=EDGE_LOOP ( 'NONE', ( #17204, #38842, #85294 ) ) ;
#20625=CARTESIAN_POINT ( 'NONE',  ( 57.48921356237308800, -27.52281430457095368, 5.000000000000000000 ) ) ;
#20627=CARTESIAN_POINT ( 'NONE',  ( 33.51665438641022376, 22.22500000000000142, 4.500000000000000888 ) ) ;
#20628=VERTEX_POINT ( 'NONE', #57599 ) ;
#20629=CARTESIAN_POINT ( 'NONE',  ( -34.82816939922328459, 18.75929247661553134, 4.000000000000000000 ) ) ;
#20630=ORIENTED_EDGE ( 'NONE', *, *, #29720, .T. ) ;
#20631=ORIENTED_EDGE ( 'NONE', *, *, #117298, .F. ) ;
#20632=VERTEX_POINT ( 'NONE', #101786 ) ;
#20633=DIRECTION ( 'NONE',  ( -0.000000000000000000, -0.3543493200069152693, 0.9351131265310292928 ) ) ;
#20636=VECTOR ( 'NONE', #27086, 1000.000000000000227 ) ;
#20637=VECTOR ( 'NONE', #48203, 999.9999999999998863 ) ;
#20638=LINE ( 'NONE', #119930, #90108 ) ;
#20639=LINE ( 'NONE', #141745, #134807 ) ;
#20641=DIRECTION ( 'NONE',  ( -0.7071067811865486830, -0.7071067811865464625, 0.000000000000000000 ) ) ;
#20642=EDGE_CURVE ( 'NONE', #20115, #3959, #34395, .T. ) ;
#20643=LINE ( 'NONE', #33005, #140946 ) ;
#20645=FACE_OUTER_BOUND ( 'NONE', #4714, .T. ) ;
#20646=EDGE_CURVE ( 'NONE', #103659, #126053, #46757, .T. ) ;
#20648=VECTOR ( 'NONE', #85567, 1000.000000000000227 ) ;
#20649=LINE ( 'NONE', #87358, #70312 ) ;
#20650=DIRECTION ( 'NONE',  ( -0.7071067811865487940, 0.7071067811865463515, 0.000000000000000000 ) ) ;
#20651=ORIENTED_EDGE ( 'NONE', *, *, #109350, .F. ) ;
#20652=LINE ( 'NONE', #96069, #34423 ) ;
#20653=PLANE ( 'NONE',  #109207 ) ;
#20654=ORIENTED_EDGE ( 'NONE', *, *, #3760, .F. ) ;
#20655=ORIENTED_EDGE ( 'NONE', *, *, #100375, .F. ) ;
#20656=DIRECTION ( 'NONE',  ( 0.3543493200069162685, -0.000000000000000000, -0.9351131265310288487 ) ) ;
#20657=CARTESIAN_POINT ( 'NONE',  ( -29.20666063542132207, 21.75929247661549226, 4.998822639870711626 ) ) ;
#20658=PLANE ( 'NONE',  #84027 ) ;
#20659=AXIS2_PLACEMENT_3D ( 'NONE', #68678, #70823, #104104 ) ;
#20662=PLANE ( 'NONE',  #25045 ) ;
#20664=EDGE_CURVE ( 'NONE', #125758, #97364, #122096, .T. ) ;
#20665=FACE_OUTER_BOUND ( 'NONE', #28382, .T. ) ;
#20666=VECTOR ( 'NONE', #120523, 1000.000000000000000 ) ;
#20667=PLANE ( 'NONE',  #53061 ) ;
#20668=EDGE_CURVE ( 'NONE', #123227, #3179, #35863, .T. ) ;
#20669=FACE_OUTER_BOUND ( 'NONE', #62637, .T. ) ;
#20671=VERTEX_POINT ( 'NONE', #80079 ) ;
#20673=EDGE_LOOP ( 'NONE', ( #115253, #55507, #37706, #39695 ) ) ;
#20674=CARTESIAN_POINT ( 'NONE',  ( -6.183988606268994381, 28.73617430169791476, 5.000000000000000000 ) ) ;
#20675=PLANE ( 'NONE',  #98505 ) ;
#20677=AXIS2_PLACEMENT_3D ( 'NONE', #130612, #41425, #97201 ) ;
#20678=AXIS2_PLACEMENT_3D ( 'NONE', #67814, #142488, #112002 ) ;
#20680=DIRECTION ( 'NONE',  ( -0.7071067811865487940, 0.7071067811865463515, -0.000000000000000000 ) ) ;
#20681=FACE_OUTER_BOUND ( 'NONE', #67045, .T. ) ;
#20682=VERTEX_POINT ( 'NONE', #102529 ) ;
#20684=EDGE_CURVE ( 'NONE', #2974, #44911, #79377, .T. ) ;
#20686=CARTESIAN_POINT ( 'NONE',  ( -45.18398860626900415, 28.73617430169818832, 5.000000000000000000 ) ) ;
#20687=ORIENTED_EDGE ( 'NONE', *, *, #128065, .F. ) ;
#20688=ORIENTED_EDGE ( 'NONE', *, *, #119837, .T. ) ;
#20689=DIRECTION ( 'NONE',  ( -0.000000000000000000, -0.3543493200069152693, 0.9351131265310292928 ) ) ;
#20691=VECTOR ( 'NONE', #141971, 999.9999999999998863 ) ;
#20692=VECTOR ( 'NONE', #97494, 1000.000000000000227 ) ;
#20693=DIRECTION ( 'NONE',  ( -0.7071067811865487940, 0.7071067811865463515, 0.000000000000000000 ) ) ;
#20694=DIRECTION ( 'NONE',  ( -1.000000000000000000, 0.000000000000000000, -0.000000000000000000 ) ) ;
#20696=FACE_OUTER_BOUND ( 'NONE', #18329, .T. ) ;
#20698=ORIENTED_EDGE ( 'NONE', *, *, #61850, .T. ) ;
#20699=CARTESIAN_POINT ( 'NONE',  ( -78.29974487139158157, -27.71228299555260577, 4.000000000000000000 ) ) ;
#20700=DIRECTION ( 'NONE',  ( 0.6830127018922180770, -0.6830127018922204085, -0.2588190451025213501 ) ) ;
#20702=VECTOR ( 'NONE', #131401, 1000.000000000000000 ) ;
#20703=ORIENTED_EDGE ( 'NONE', *, *, #33250, .F. ) ;
#20705=ORIENTED_EDGE ( 'NONE', *, *, #110949, .F. ) ;
#20708=EDGE_CURVE ( 'NONE', #73712, #56655, #124255, .T. ) ;
#20709=LINE ( 'NONE', #86713, #135027 ) ;
#20710=ORIENTED_EDGE ( 'NONE', *, *, #85678, .F. ) ;
#20712=DIRECTION ( 'NONE',  ( 0.7071067811865487940, -0.7071067811865463515, 0.000000000000000000 ) ) ;
#20713=CARTESIAN_POINT ( 'NONE',  ( 39.48921356237310221, -27.52281430457082934, 5.000000000000000000 ) ) ;
#20715=EDGE_CURVE ( 'NONE', #115411, #63259, #67030, .T. ) ;
#20716=CARTESIAN_POINT ( 'NONE',  ( -51.48921356237309510, -27.52281430457091460, 5.000000000000000000 ) ) ;
#20717=ORIENTED_EDGE ( 'NONE', *, *, #112141, .F. ) ;
#20718=FACE_OUTER_BOUND ( 'NONE', #104599, .T. ) ;
#20719=CARTESIAN_POINT ( 'NONE',  ( 6.995075227788017713, -5.240707523384232402, 12.38332538355494172 ) ) ;
#20720=CARTESIAN_POINT ( 'NONE',  ( 23.36654548503486950, 7.297668562427137573, 4.000000000000000000 ) ) ;
#20722=EDGE_LOOP ( 'NONE', ( #37945, #88592, #43529, #2790 ) ) ;
#20724=ORIENTED_EDGE ( 'NONE', *, *, #141367, .T. ) ;
#20725=EDGE_CURVE ( 'NONE', #121857, #25213, #69179, .T. ) ;
#20728=EDGE_CURVE ( 'NONE', #69796, #18367, #80771, .T. ) ;
#20729=DIRECTION ( 'NONE',  ( -0.7071067811865487940, 0.7071067811865463515, 0.000000000000000000 ) ) ;
#20730=CARTESIAN_POINT ( 'NONE',  ( 48.29974487139158867, -27.71228299555239971, 4.000000000000000000 ) ) ;
#20732=LINE ( 'NONE', #20010, #126726 ) ;
#20734=VERTEX_POINT ( 'NONE', #122831 ) ;
#20735=EDGE_CURVE ( 'NONE', #29818, #67807, #1715, .T. ) ;
#20736=CARTESIAN_POINT ( 'NONE',  ( 6.005480084712508493, 28.92564299267933947, 4.000000000000000000 ) ) ;
#20737=EDGE_CURVE ( 'NONE', #116339, #96152, #69924, .T. ) ;
#20738=ORIENTED_EDGE ( 'NONE', *, *, #73571, .T. ) ;
#20739=EDGE_CURVE ( 'NONE', #119532, #139613, #55443, .T. ) ;
#20742=AXIS2_PLACEMENT_3D ( 'NONE', #53065, #32048, #108144 ) ;
#20743=AXIS2_PLACEMENT_3D ( 'NONE', #28709, #137460, #72953 ) ;
#20744=VECTOR ( 'NONE', #41240, 1000.000000000000000 ) ;
#20745=EDGE_LOOP ( 'NONE', ( #113299, #123864, #16675, #22529 ) ) ;
#20746=ORIENTED_EDGE ( 'NONE', *, *, #82795, .F. ) ;
#20747=AXIS2_PLACEMENT_3D ( 'NONE', #69876, #23466, #122779 ) ;
#20748=EDGE_CURVE ( 'NONE', #140112, #55587, #302, .T. ) ;
#20749=EDGE_CURVE ( 'NONE', #75175, #23274, #44604, .T. ) ;
#20750=DIRECTION ( 'NONE',  ( -0.7071067811865486830, 0.7071067811865464625, 0.000000000000000000 ) ) ;
#20752=CARTESIAN_POINT ( 'NONE',  ( 26.99999999999981881, 11.96639925780213609, 5.000000000000000000 ) ) ;
#20754=CARTESIAN_POINT ( 'NONE',  ( -25.25154412867560438, -11.24070752338416845, 10.39518518046015139 ) ) ;
#20755=EDGE_CURVE ( 'NONE', #30838, #28258, #1024, .T. ) ;
#20756=CARTESIAN_POINT ( 'NONE',  ( 23.99999999999983302, -8.731860332648819778, -2.120594902707481744 ) ) ;
#20758=VECTOR ( 'NONE', #121912, 1000.000000000000227 ) ;
#20759=ORIENTED_EDGE ( 'NONE', *, *, #131723, .T. ) ;
#20762=ORIENTED_EDGE ( 'NONE', *, *, #87695, .T. ) ;
#20763=CIRCLE ( 'NONE', #101803, 5.968999999999998529 ) ;
#20766=( BOUNDED_CURVE ( )  B_SPLINE_CURVE ( 3, ( #96364, #52179, #28306, #140606 ),
 .UNSPECIFIED., .F., .F. ) 
 B_SPLINE_CURVE_WITH_KNOTS ( ( 4, 4 ),
 ( 4.350170835173037709, 4.500739107949217832 ),
 .UNSPECIFIED. ) 
 CURVE ( )  GEOMETRIC_REPRESENTATION_ITEM ( )  RATIONAL_B_SPLINE_CURVE ( ( 1.000000000000000000, 0.9981116584018958626, 0.9981116584018958626, 1.000000000000000000 ) ) 
 REPRESENTATION_ITEM ( '' )  );
#20767=CARTESIAN_POINT ( 'NONE',  ( -5.510786437626906675, -27.52281430457051314, 5.000000000000000000 ) ) ;
#20768=AXIS2_PLACEMENT_3D ( 'NONE', #66555, #128431, #29104 ) ;
#20769=LINE ( 'NONE', #65022, #26290 ) ;
#20770=ORIENTED_EDGE ( 'NONE', *, *, #118824, .F. ) ;
#20771=DIRECTION ( 'NONE',  ( -0.000000000000000000, -0.3543493200069152693, 0.9351131265310292928 ) ) ;
#20772=DIRECTION ( 'NONE',  ( 0.7071067811865487940, -0.7071067811865463515, 0.000000000000000000 ) ) ;
#20773=PLANE ( 'NONE',  #29612 ) ;
#20776=VECTOR ( 'NONE', #42889, 1000.000000000000227 ) ;
#20777=LINE ( 'NONE', #9143, #49149 ) ;
#20778=ORIENTED_EDGE ( 'NONE', *, *, #84282, .F. ) ;
#20779=LINE ( 'NONE', #74484, #17135 ) ;
#20781=VECTOR ( 'NONE', #57996, 1000.000000000000000 ) ;
#20782=EDGE_LOOP ( 'NONE', ( #87112, #13999, #31338, #112756 ) ) ;
#20783=ORIENTED_EDGE ( 'NONE', *, *, #129091, .F. ) ;
#20785=ORIENTED_EDGE ( 'NONE', *, *, #7200, .F. ) ;
#20787=VECTOR ( 'NONE', #2492, 1000.000000000000000 ) ;
#20788=VERTEX_POINT ( 'NONE', #35135 ) ;
#20789=EDGE_CURVE ( 'NONE', #54960, #44135, #89481, .T. ) ;
#20790=DIRECTION ( 'NONE',  ( 0.6830127018922180770, -0.6830127018922204085, -0.2588190451025213501 ) ) ;
#20791=CARTESIAN_POINT ( 'NONE',  ( -18.18398860626898994, 28.73617430169800002, 5.000000000000000000 ) ) ;
#20793=CARTESIAN_POINT ( 'NONE',  ( -63.48921356237309510, -27.52281430457099631, 5.000000000000000000 ) ) ;
#20797=ORIENTED_EDGE ( 'NONE', *, *, #60978, .F. ) ;
#20798=CARTESIAN_POINT ( 'NONE',  ( 4.499999999999972466, 8.900465351122155866, -2.516491619111523192 ) ) ;
#20800=CARTESIAN_POINT ( 'NONE',  ( 15.27825451568563864, 8.259292476615637923, 11.78515199841153738 ) ) ;
#20801=LINE ( 'NONE', #62920, #67662 ) ;
#20802=DIRECTION ( 'NONE',  ( 0.6830127018922181881, 0.6830127018922202975, -0.2588190451025214056 ) ) ;
#20803=VERTEX_POINT ( 'NONE', #61879 ) ;
#20804=EDGE_CURVE ( 'NONE', #56431, #98546, #104638, .T. ) ;
#20805=ORIENTED_EDGE ( 'NONE', *, *, #90278, .F. ) ;
#20806=ORIENTED_EDGE ( 'NONE', *, *, #131462, .T. ) ;
#20807=ORIENTED_EDGE ( 'NONE', *, *, #129401, .F. ) ;
#20809=ORIENTED_EDGE ( 'NONE', *, *, #28124, .F. ) ;
#20810=VECTOR ( 'NONE', #119049, 1000.000000000000000 ) ;
#20811=CARTESIAN_POINT ( 'NONE',  ( -12.29974487139158512, -27.71228299555214747, 4.000000000000000000 ) ) ;
#20812=EDGE_CURVE ( 'NONE', #14007, #142960, #136545, .T. ) ;
#20813=CARTESIAN_POINT ( 'NONE',  ( 0.000000000000000000, 0.000000000000000000, 5.000000000000000000 ) ) ;
#20814=ORIENTED_EDGE ( 'NONE', *, *, #7771, .T. ) ;
#20815=DIRECTION ( 'NONE',  ( 0.7071067811865487940, 0.7071067811865463515, -0.000000000000000000 ) ) ;
#20816=ORIENTED_EDGE ( 'NONE', *, *, #34704, .F. ) ;
#20818=DIRECTION ( 'NONE',  ( -0.7071067811865486830, -0.7071067811865464625, -0.000000000000000000 ) ) ;
#20819=DIRECTION ( 'NONE',  ( 0.7071067811865486830, -0.7071067811865464625, -0.000000000000000000 ) ) ;
#20821=EDGE_LOOP ( 'NONE', ( #69813, #78266, #131174, #139786 ) ) ;
#20822=EDGE_LOOP ( 'NONE', ( #142693, #35012, #97498, #98542 ) ) ;
#20826=PLANE ( 'NONE',  #105208 ) ;
#20827=PLANE ( 'NONE',  #136248 ) ;
#20828=CARTESIAN_POINT ( 'NONE',  ( -29.99451991528749417, 28.92564299267958816, 4.000000000000000000 ) ) ;
#20829=VECTOR ( 'NONE', #136714, 1000.000000000000000 ) ;
#20830=CARTESIAN_POINT ( 'NONE',  ( 24.18398860626899705, 28.73617430169804265, 5.000000000000000000 ) ) ;
#20831=EDGE_CURVE ( 'NONE', #22070, #124953, #137289, .T. ) ;
#20833=CARTESIAN_POINT ( 'NONE',  ( -0.3165796113278919188, -6.740707523384209310, 11.88629033278124503 ) ) ;
#20834=LINE ( 'NONE', #125160, #41936 ) ;
#20839=AXIS2_PLACEMENT_3D ( 'NONE', #26037, #70298, #81141 ) ;
#20840=VECTOR ( 'NONE', #24048, 1000.000000000000000 ) ;
#20841=CARTESIAN_POINT ( 'NONE',  ( -33.48921356237309510, -27.52281430457078670, 5.000000000000000000 ) ) ;
#20842=VERTEX_POINT ( 'NONE', #128547 ) ;
#20843=VECTOR ( 'NONE', #44370, 1000.000000000000000 ) ;
#20844=CARTESIAN_POINT ( 'NONE',  ( -19.05000000000000071, 3.174999999999997158, 5.000000000000000000 ) ) ;
#20845=CARTESIAN_POINT ( 'NONE',  ( 4.499999999999970690, -13.91253812416061386, 4.000000000000000000 ) ) ;
#20846=ORIENTED_EDGE ( 'NONE', *, *, #88302, .T. ) ;
#20848=FACE_OUTER_BOUND ( 'NONE', #101353, .T. ) ;
#20850=VERTEX_POINT ( 'NONE', #83640 ) ;
#20851=CARTESIAN_POINT ( 'NONE',  ( -27.18398860626900060, 28.73617430169806042, 5.000000000000000000 ) ) ;
#20853=ORIENTED_EDGE ( 'NONE', *, *, #93635, .T. ) ;
#20857=CARTESIAN_POINT ( 'NONE',  ( -44.99451991528749772, 28.92564299267969474, 4.000000000000000000 ) ) ;
#20858=DIRECTION ( 'NONE',  ( -0.7071067811865486830, -0.7071067811865464625, 0.000000000000000000 ) ) ;
#20859=DIRECTION ( 'NONE',  ( 0.7071067811865486830, -0.7071067811865464625, -0.000000000000000000 ) ) ;
#20860=CARTESIAN_POINT ( 'NONE',  ( 21.48921356237309155, -27.52281430457070499, 5.000000000000000000 ) ) ;
#20863=VECTOR ( 'NONE', #6388, 1000.000000000000000 ) ;
#20864=DIRECTION ( 'NONE',  ( 0.7071067811865487940, 0.7071067811865463515, -0.000000000000000000 ) ) ;
#20865=CARTESIAN_POINT ( 'NONE',  ( 8.292893218813395251, 17.25929247661554911, 5.000000000000000000 ) ) ;
#20866=VERTEX_POINT ( 'NONE', #50277 ) ;
#20867=ORIENTED_EDGE ( 'NONE', *, *, #38603, .F. ) ;
#20868=VECTOR ( 'NONE', #8903, 999.9999999999998863 ) ;
#20869=DIRECTION ( 'NONE',  ( 0.000000000000000000, 1.000000000000000000, -0.000000000000000000 ) ) ;
#20870=EDGE_LOOP ( 'NONE', ( #47095, #79821, #115699, #848 ) ) ;
#20872=CARTESIAN_POINT ( 'NONE',  ( -34.92500000000001137, -22.22500000000000142, 4.000000000000000000 ) ) ;
#20873=CARTESIAN_POINT ( 'NONE',  ( -0.005480084712502889671, 28.92564299267938210, 4.000000000000000000 ) ) ;
#20874=CARTESIAN_POINT ( 'NONE',  ( 34.42499999999998295, 20.97718569542917777, 5.000000000000000000 ) ) ;
#20875=VERTEX_POINT ( 'NONE', #28530 ) ;
#20876=VECTOR ( 'NONE', #136969, 1000.000000000000000 ) ;
#20877=CARTESIAN_POINT ( 'NONE',  ( 11.51078643762690490, -27.52281430457047406, 5.000000000000000000 ) ) ;
#20878=CARTESIAN_POINT ( 'NONE',  ( -34.42500000000001137, 0.000000000000000000, 4.500000000000000888 ) ) ;
#20879=CARTESIAN_POINT ( 'NONE',  ( -48.18398860626899705, 28.73617430169820608, 5.000000000000000000 ) ) ;
#20880=FACE_OUTER_BOUND ( 'NONE', #126952, .T. ) ;
#20881=VECTOR ( 'NONE', #85202, 999.9999999999998863 ) ;
#20883=DIRECTION ( 'NONE',  ( 0.7071067811865487940, 0.7071067811865463515, 0.000000000000000000 ) ) ;
#20884=ORIENTED_EDGE ( 'NONE', *, *, #74135, .F. ) ;
#20885=CARTESIAN_POINT ( 'NONE',  ( -9.792893218813388145, -2.240707523384257716, 5.000000000000000000 ) ) ;
#20887=CARTESIAN_POINT ( 'NONE',  ( -3.489213562373097322, -27.52281430457057709, 5.000000000000000000 ) ) ;
#20888=PLANE ( 'NONE',  #58620 ) ;
#20889=ORIENTED_EDGE ( 'NONE', *, *, #41118, .F. ) ;
#20890=EDGE_LOOP ( 'NONE', ( #46424, #32225, #33089, #10114 ) ) ;
#20891=ORIENTED_EDGE ( 'NONE', *, *, #82760, .T. ) ;
#20892=EDGE_CURVE ( 'NONE', #124072, #93762, #139456, .T. ) ;
#20895=ORIENTED_EDGE ( 'NONE', *, *, #12027, .F. ) ;
#20897=CARTESIAN_POINT ( 'NONE',  ( 21.79333936457832266, 21.75929247661549226, 4.998822639870715179 ) ) ;
#20898=EDGE_CURVE ( 'NONE', #99900, #46818, #82215, .T. ) ;
#20899=AXIS2_PLACEMENT_3D ( 'NONE', #78482, #66889, #134296 ) ;
#20900=EDGE_LOOP ( 'NONE', ( #133613, #108987, #28886, #795 ) ) ;
#20905=EDGE_LOOP ( 'NONE', ( #81602, #79944, #50641, #109015 ) ) ;
#20906=LINE ( 'NONE', #54302, #120734 ) ;
#20908=VECTOR ( 'NONE', #84830, 1000.000000000000227 ) ;
#20909=ORIENTED_EDGE ( 'NONE', *, *, #38996, .T. ) ;
#20910=ORIENTED_EDGE ( 'NONE', *, *, #77573, .F. ) ;
#20911=EDGE_CURVE ( 'NONE', #136433, #125587, #126385, .T. ) ;
#20912=ORIENTED_EDGE ( 'NONE', *, *, #74609, .F. ) ;
#20913=DIRECTION ( 'NONE',  ( -0.7071067811865486830, 0.7071067811865464625, 0.000000000000000000 ) ) ;
#20914=EDGE_CURVE ( 'NONE', #43938, #125881, #94467, .T. ) ;
#20915=CARTESIAN_POINT ( 'NONE',  ( -54.18398860626899705, 28.73617430169825226, 5.000000000000000000 ) ) ;
#20917=LINE ( 'NONE', #110766, #37310 ) ;
#20919=DIRECTION ( 'NONE',  ( 0.3543493200069162685, -0.000000000000000000, -0.9351131265310288487 ) ) ;
#20920=ADVANCED_FACE ( 'NONE', ( #103901 ), #48137, .F. ) ;
#20922=SURFACE_STYLE_FILL_AREA ( #139175 ) ;
#20923=ORIENTED_EDGE ( 'NONE', *, *, #111149, .T. ) ;
#20925=ORIENTED_EDGE ( 'NONE', *, *, #26688, .F. ) ;
#20926=DIRECTION ( 'NONE',  ( -0.6830127018922181881, 0.6830127018922202975, -0.2588190451025214056 ) ) ;
#20927=ORIENTED_EDGE ( 'NONE', *, *, #96818, .T. ) ;
#20928=ORIENTED_EDGE ( 'NONE', *, *, #22211, .F. ) ;
#20931=AXIS2_PLACEMENT_3D ( 'NONE', #38061, #59131, #138803 ) ;
#20932=CARTESIAN_POINT ( 'NONE',  ( 15.18398860626900237, 28.73617430169797871, 5.000000000000000000 ) ) ;
#20933=ORIENTED_EDGE ( 'NONE', *, *, #63964, .T. ) ;
#20934=CARTESIAN_POINT ( 'NONE',  ( 45.18398860626900415, 28.73617430169818832, 5.000000000000000000 ) ) ;
#20936=CARTESIAN_POINT ( 'NONE',  ( -23.99999999999983302, 13.93112307739204425, 4.000000000000000000 ) ) ;
#20937=EDGE_CURVE ( 'NONE', #49762, #74191, #30673, .T. ) ;
#20938=FACE_OUTER_BOUND ( 'NONE', #130709, .T. ) ;
#20939=AXIS2_PLACEMENT_3D ( 'NONE', #43466, #88417, #66657 ) ;
#20943=ORIENTED_EDGE ( 'NONE', *, *, #112698, .F. ) ;
#20944=VECTOR ( 'NONE', #140774, 1000.000000000000000 ) ;
#20945=CARTESIAN_POINT ( 'NONE',  ( 17.99999999999987566, 13.93112307739204425, 4.000000000000000000 ) ) ;
#20946=ORIENTED_EDGE ( 'NONE', *, *, #66917, .F. ) ;
#20948=ORIENTED_EDGE ( 'NONE', *, *, #12634, .T. ) ;
#20949=DIRECTION ( 'NONE',  ( 0.7071067811865486830, -0.7071067811865464625, -0.000000000000000000 ) ) ;
#20950=VERTEX_POINT ( 'NONE', #53859 ) ;
#20951=LINE ( 'NONE', #43437, #8809 ) ;
#20952=ORIENTED_EDGE ( 'NONE', *, *, #108637, .F. ) ;
#20953=VERTEX_POINT ( 'NONE', #21197 ) ;
#20954=VECTOR ( 'NONE', #60146, 1000.000000000000000 ) ;
#20955=EDGE_LOOP ( 'NONE', ( #49144, #24771, #44806, #127232 ) ) ;
#20956=ADVANCED_FACE ( 'NONE', ( #40822 ), #74166, .F. ) ;
#20957=PLANE ( 'NONE',  #257 ) ;
#20958=CARTESIAN_POINT ( 'NONE',  ( 24.79593897580385331, 4.791522900035168675, 4.000000000000000000 ) ) ;
#20959=FACE_OUTER_BOUND ( 'NONE', #142818, .T. ) ;
#20961=PLANE ( 'NONE',  #28912 ) ;
#20962=FACE_OUTER_BOUND ( 'NONE', #117845, .T. ) ;
#20963=DIRECTION ( 'NONE',  ( -0.7071067811865486830, -0.7071067811865464625, 0.000000000000000000 ) ) ;
#20964=VECTOR ( 'NONE', #72971, 1000.000000000000227 ) ;
#20965=LINE ( 'NONE', #12231, #109455 ) ;
#20966=VECTOR ( 'NONE', #2744, 1000.000000000000000 ) ;
#20967=LINE ( 'NONE', #9346, #36723 ) ;
#20968=AXIS2_PLACEMENT_3D ( 'NONE', #53799, #33484, #140765 ) ;
#20970=LINE ( 'NONE', #75377, #40127 ) ;
#20971=EDGE_CURVE ( 'NONE', #24063, #78218, #106766, .T. ) ;
#20972=ORIENTED_EDGE ( 'NONE', *, *, #50816, .T. ) ;
#20973=AXIS2_PLACEMENT_3D ( 'NONE', #43009, #141602, #88660 ) ;
#20975=ORIENTED_EDGE ( 'NONE', *, *, #5932, .F. ) ;
#20976=PLANE ( 'NONE',  #114343 ) ;
#20977=EDGE_LOOP ( 'NONE', ( #113471, #52075 ) ) ;
#20979=ORIENTED_EDGE ( 'NONE', *, *, #55629, .F. ) ;
#20980=CARTESIAN_POINT ( 'NONE',  ( -15.18398860626900237, 28.73617430169797871, 5.000000000000000000 ) ) ;
#20981=CARTESIAN_POINT ( 'NONE',  ( 18.48921356237309510, -27.52281430457068367, 5.000000000000000000 ) ) ;
#20982=EDGE_CURVE ( 'NONE', #129488, #98003, #140818, .T. ) ;
#20983=VECTOR ( 'NONE', #118370, 1000.000000000000227 ) ;
#20984=CARTESIAN_POINT ( 'NONE',  ( -34.92500000000001137, 22.22500000000000142, 4.000000000000000000 ) ) ;
#20985=ORIENTED_EDGE ( 'NONE', *, *, #37283, .T. ) ;
#20986=PLANE ( 'NONE',  #67305 ) ;
#20987=EDGE_LOOP ( 'NONE', ( #55607, #51871, #126124, #45801 ) ) ;
#20988=CARTESIAN_POINT ( 'NONE',  ( -21.18398860626899349, 28.73617430169802134, 5.000000000000000000 ) ) ;
#20989=DIRECTION ( 'NONE',  ( 0.7071067811865487940, 0.7071067811865463515, 0.000000000000000000 ) ) ;
#20990=VECTOR ( 'NONE', #74370, 1000.000000000000000 ) ;
#20995=FACE_OUTER_BOUND ( 'NONE', #91394, .T. ) ;
#20996=DIRECTION ( 'NONE',  ( -0.000000000000000000, 0.000000000000000000, 1.000000000000000000 ) ) ;
#20997=EDGE_LOOP ( 'NONE', ( #58818, #85114, #112359, #84989 ) ) ;
#20999=ORIENTED_EDGE ( 'NONE', *, *, #136417, .F. ) ;
#21001=AXIS2_PLACEMENT_3D ( 'NONE', #116806, #63186, #8023 ) ;
#21002=EDGE_LOOP ( 'NONE', ( #131038, #138536, #12569, #67117 ) ) ;
#21003=LINE ( 'NONE', #86291, #13897 ) ;
#21004=DIRECTION ( 'NONE',  ( -0.7071067811865486830, -0.7071067811865464625, 0.000000000000000000 ) ) ;
#21005=FACE_OUTER_BOUND ( 'NONE', #109700, .T. ) ;
#21008=EDGE_CURVE ( 'NONE', #56060, #102325, #97298, .T. ) ;
#21009=CARTESIAN_POINT ( 'NONE',  ( -36.48921356237310221, -27.52281430457080802, 5.000000000000000000 ) ) ;
#21010=ORIENTED_EDGE ( 'NONE', *, *, #7792, .T. ) ;
#21011=DIRECTION ( 'NONE',  ( 0.7071067811865487940, -0.7071067811865463515, 0.000000000000000000 ) ) ;
#21013=DIRECTION ( 'NONE',  ( -0.3543493200069163240, 0.000000000000000000, 0.9351131265310288487 ) ) ;
#21015=EDGE_CURVE ( 'NONE', #88631, #6614, #109632, .T. ) ;
#21017=VERTEX_POINT ( 'NONE', #87172 ) ;
#21019=EDGE_CURVE ( 'NONE', #110441, #38956, #51712, .T. ) ;
#21020=DIRECTION ( 'NONE',  ( -0.7071067811865487940, 0.7071067811865463515, 0.000000000000000000 ) ) ;
#21021=DIRECTION ( 'NONE',  ( 0.7071067811865486830, -0.7071067811865464625, -0.000000000000000000 ) ) ;
#21022=AXIS2_PLACEMENT_3D ( 'NONE', #79948, #100931, #34996 ) ;
#21023=EDGE_LOOP ( 'NONE', ( #27264, #128030, #90952, #51082 ) ) ;
#21025=CARTESIAN_POINT ( 'NONE',  ( 8.999999999999948486, 11.58746187583912324, 4.000000000000000000 ) ) ;
#21026=CARTESIAN_POINT ( 'NONE',  ( 63.29974487139158867, -27.71228299555250274, 4.000000000000000000 ) ) ;
#21028=PLANE ( 'NONE',  #99849 ) ;
#21029=PLANE ( 'NONE',  #30554 ) ;
#21031=CARTESIAN_POINT ( 'NONE',  ( 6.299744871391586898, -27.71228299555210484, 4.000000000000000000 ) ) ;
#21032=DIRECTION ( 'NONE',  ( 0.6830127018922181881, 0.6830127018922202975, -0.2588190451025214056 ) ) ;
#21036=DIRECTION ( 'NONE',  ( 0.3543493200069162685, -0.000000000000000000, -0.9351131265310288487 ) ) ;
#21037=ORIENTED_EDGE ( 'NONE', *, *, #7751, .F. ) ;
#21038=ADVANCED_FACE ( 'NONE', ( #8837 ), #142290, .T. ) ;
#21039=ORIENTED_EDGE ( 'NONE', *, *, #85365, .F. ) ;
#21040=ORIENTED_EDGE ( 'NONE', *, *, #66440, .T. ) ;
#21044=ORIENTED_EDGE ( 'NONE', *, *, #100632, .T. ) ;
#21045=ORIENTED_EDGE ( 'NONE', *, *, #34532, .F. ) ;
#21046=ORIENTED_EDGE ( 'NONE', *, *, #97206, .F. ) ;
#21047=DIRECTION ( 'NONE',  ( 0.7071067811865486830, -0.7071067811865464625, -0.000000000000000000 ) ) ;
#21048=CARTESIAN_POINT ( 'NONE',  ( -23.67183060077630685, -18.74070752338409918, 4.000000000000000000 ) ) ;
#21049=VECTOR ( 'NONE', #48847, 1000.000000000000000 ) ;
#21051=VECTOR ( 'NONE', #81682, 999.9999999999998863 ) ;
#21052=EDGE_LOOP ( 'NONE', ( #64114, #20975, #33982, #105791 ) ) ;
#21053=CARTESIAN_POINT ( 'NONE',  ( 12.75860074219786711, 21.72500000000000142, 5.000000000000000000 ) ) ;
#21057=DIRECTION ( 'NONE',  ( 1.000000000000000000, -0.000000000000000000, 0.000000000000000000 ) ) ;
#21060=PLANE ( 'NONE',  #3337 ) ;
#21061=VECTOR ( 'NONE', #13561, 1000.000000000000000 ) ;
#21063=LINE ( 'NONE', #43545, #19062 ) ;
#21064=DIRECTION ( 'NONE',  ( -0.6830127018922181881, 0.6830127018922202975, -0.2588190451025214056 ) ) ;
#21066=CARTESIAN_POINT ( 'NONE',  ( 83.99451991528748351, 28.92564299267996830, 4.000000000000000000 ) ) ;
#21067=EDGE_CURVE ( 'NONE', #103751, #105472, #52393, .T. ) ;
#21069=VERTEX_POINT ( 'NONE', #42266 ) ;
#21070=ADVANCED_FACE ( 'NONE', ( #32083 ), #130707, .F. ) ;
#21072=ORIENTED_EDGE ( 'NONE', *, *, #78533, .F. ) ;
#21075=EDGE_CURVE ( 'NONE', #16081, #139077, #42977, .T. ) ;
#21076=VECTOR ( 'NONE', #106590, 1000.000000000000000 ) ;
#21077=CARTESIAN_POINT ( 'NONE',  ( 29.30673006690383176, -3.740707523384248390, 12.88036043432860822 ) ) ;
#21078=LINE ( 'NONE', #65346, #129011 ) ;
#21079=DIRECTION ( 'NONE',  ( 0.6830127018922180770, -0.6830127018922204085, -0.2588190451025213501 ) ) ;
#21080=EDGE_CURVE ( 'NONE', #89257, #67554, #54567, .T. ) ;
#21083=FACE_OUTER_BOUND ( 'NONE', #35476, .T. ) ;
#21085=VECTOR ( 'NONE', #82972, 1000.000000000000000 ) ;
#21087=VERTEX_POINT ( 'NONE', #62582 ) ;
#21088=VECTOR ( 'NONE', #113686, 1000.000000000000000 ) ;
#21089=ORIENTED_EDGE ( 'NONE', *, *, #92244, .F. ) ;
#21090=DIRECTION ( 'NONE',  ( -0.000000000000000000, 0.000000000000000000, 1.000000000000000000 ) ) ;
#21091=VECTOR ( 'NONE', #118191, 1000.000000000000227 ) ;
#21092=CARTESIAN_POINT ( 'NONE',  ( -59.99451991528749772, 28.92564299267980132, 4.000000000000000000 ) ) ;
#21093=EDGE_LOOP ( 'NONE', ( #129, #64610, #45669, #70940 ) ) ;
#21095=EDGE_CURVE ( 'NONE', #12281, #110799, #129235, .T. ) ;
#21096=EDGE_LOOP ( 'NONE', ( #39311, #38509, #29018, #34186 ) ) ;
#21097=VECTOR ( 'NONE', #77595, 1000.000000000000000 ) ;
#21098=LINE ( 'NONE', #55176, #79576 ) ;
#21099=ADVANCED_FACE ( 'NONE', ( #118357 ), #8155, .F. ) ;
#21100=CARTESIAN_POINT ( 'NONE',  ( 11.81601139373100651, 28.73617430169779041, 5.000000000000000000 ) ) ;
#21101=DIRECTION ( 'NONE',  ( 0.7071067811865487940, 0.7071067811865463515, -0.000000000000000000 ) ) ;
#21102=VECTOR ( 'NONE', #105607, 1000.000000000000000 ) ;
#21103=EDGE_CURVE ( 'NONE', #114174, #96751, #1549, .T. ) ;
#21105=EDGE_LOOP ( 'NONE', ( #107170, #45780, #130089, #131293 ) ) ;
#21106=DIRECTION ( 'NONE',  ( 0.7071067811865487940, -0.7071067811865463515, 0.000000000000000000 ) ) ;
#21108=ORIENTED_EDGE ( 'NONE', *, *, #45413, .F. ) ;
#21109=VECTOR ( 'NONE', #67270, 1000.000000000000227 ) ;
#21110=EDGE_CURVE ( 'NONE', #65170, #78582, #100895, .T. ) ;
#21112=VECTOR ( 'NONE', #9206, 1000.000000000000227 ) ;
#21113=PLANE ( 'NONE',  #99720 ) ;
#21115=ORIENTED_EDGE ( 'NONE', *, *, #130847, .F. ) ;
#21118=EDGE_CURVE ( 'NONE', #126057, #85488, #122644, .T. ) ;
#21120=CARTESIAN_POINT ( 'NONE',  ( 0.7071067811865432429, 2.259292476615688994, 5.000000000000000000 ) ) ;
#21122=FACE_BOUND ( 'NONE', #45974, .T. ) ;
#21124=CARTESIAN_POINT ( 'NONE',  ( -5.999999999999960032, -1.068876922607802538, 4.000000000000000000 ) ) ;
#21125=CARTESIAN_POINT ( 'NONE',  ( -39.18398860626899705, 28.73617430169814568, 5.000000000000000000 ) ) ;
#21126=PLANE ( 'NONE',  #74081 ) ;
#21127=ORIENTED_EDGE ( 'NONE', *, *, #98238, .T. ) ;
#21128=EDGE_CURVE ( 'NONE', #124198, #89614, #11002, .T. ) ;
#21130=ORIENTED_EDGE ( 'NONE', *, *, #102262, .T. ) ;
#21131=EDGE_CURVE ( 'NONE', #62743, #116904, #112495, .T. ) ;
#21132=ORIENTED_EDGE ( 'NONE', *, *, #106544, .T. ) ;
#21134=LINE ( 'NONE', #69487, #86483 ) ;
#21135=ORIENTED_EDGE ( 'NONE', *, *, #1559, .F. ) ;
#21136=EDGE_CURVE ( 'NONE', #37795, #50134, #134258, .T. ) ;
#21138=ORIENTED_EDGE ( 'NONE', *, *, #18077, .F. ) ;
#21140=DIRECTION ( 'NONE',  ( 1.000000000000000000, 0.000000000000000000, 0.000000000000000000 ) ) ;
#21141=LINE ( 'NONE', #61, #101973 ) ;
#21142=EDGE_LOOP ( 'NONE', ( #73743, #118227, #111646, #10658 ) ) ;
#21145=VECTOR ( 'NONE', #133196, 1000.000000000000000 ) ;
#21147=CIRCLE ( 'NONE', #42083, 5.968999999999998529 ) ;
#21148=AXIS2_PLACEMENT_3D ( 'NONE', #1810, #80874, #70022 ) ;
#21149=CARTESIAN_POINT ( 'NONE',  ( 28.49999999999979750, -7.533600742197658739, 5.000000000000000000 ) ) ;
#21152=CARTESIAN_POINT ( 'NONE',  ( 51.48921356237309510, -27.52281430457091460, 5.000000000000000000 ) ) ;
#21153=CARTESIAN_POINT ( 'NONE',  ( 8.292986735706890045, -21.74070752338406365, 4.999753212805221558 ) ) ;
#21157=VECTOR ( 'NONE', #7089, 1000.000000000000000 ) ;
#21158=ORIENTED_EDGE ( 'NONE', *, *, #35191, .F. ) ;
#21159=AXIS2_PLACEMENT_3D ( 'NONE', #114353, #102054, #15023 ) ;
#21160=LINE ( 'NONE', #99405, #105182 ) ;
#21161=CARTESIAN_POINT ( 'NONE',  ( -60.48921356237309510, -27.52281430457097500, 5.000000000000000000 ) ) ;
#21163=VECTOR ( 'NONE', #51686, 1000.000000000000000 ) ;
#21164=ORIENTED_EDGE ( 'NONE', *, *, #122239, .T. ) ;
#21165=CARTESIAN_POINT ( 'NONE',  ( 63.48921356237309510, -27.52281430457099631, 5.000000000000000000 ) ) ;
#21166=CARTESIAN_POINT ( 'NONE',  ( 75.48921356237309510, -27.52281430457107803, 5.000000000000000000 ) ) ;
#21168=ORIENTED_EDGE ( 'NONE', *, *, #124911, .F. ) ;
#21170=PLANE ( 'NONE',  #92615 ) ;
#21171=FACE_OUTER_BOUND ( 'NONE', #97984, .T. ) ;
#21176=VECTOR ( 'NONE', #99567, 1000.000000000000000 ) ;
#21177=DIRECTION ( 'NONE',  ( 0.7071067811865487940, 0.7071067811865463515, 0.000000000000000000 ) ) ;
#21178=EDGE_CURVE ( 'NONE', #116001, #49148, #111788, .T. ) ;
#21179=CARTESIAN_POINT ( 'NONE',  ( 39.48921356237310221, -27.52281430457082934, 5.000000000000000000 ) ) ;
#21180=CARTESIAN_POINT ( 'NONE',  ( 29.99999999999979394, -0.8619312979531689178, -5.102805207349756067 ) ) ;
#21181=ORIENTED_EDGE ( 'NONE', *, *, #17957, .F. ) ;
#21183=ORIENTED_EDGE ( 'NONE', *, *, #108799, .F. ) ;
#21184=LINE ( 'NONE', #55256, #127968 ) ;
#21185=CARTESIAN_POINT ( 'NONE',  ( -33.48921356237309510, -27.52281430457078670, 5.000000000000000000 ) ) ;
#21186=ORIENTED_EDGE ( 'NONE', *, *, #107466, .F. ) ;
#21188=VECTOR ( 'NONE', #107210, 1000.000000000000000 ) ;
#21189=AXIS2_PLACEMENT_3D ( 'NONE', #22205, #43284, #109944 ) ;
#21190=CARTESIAN_POINT ( 'NONE',  ( 11.20710678118646442, -17.24070752338410983, 5.000000000000000000 ) ) ;
#21191=CARTESIAN_POINT ( 'NONE',  ( 36.18398860626899705, 28.73617430169812437, 5.000000000000000000 ) ) ;
#21192=ORIENTED_EDGE ( 'NONE', *, *, #108301, .F. ) ;
#21193=CARTESIAN_POINT ( 'NONE',  ( -6.005480084712508493, 28.92564299267933947, 4.000000000000000000 ) ) ;
#21195=DIRECTION ( 'NONE',  ( 0.7071067811865487940, 0.7071067811865463515, 0.000000000000000000 ) ) ;
#21196=EDGE_LOOP ( 'NONE', ( #76379, #25365, #22746, #58093 ) ) ;
#21197=CARTESIAN_POINT ( 'NONE',  ( -11.20710678118645731, -11.24070752338416845, 5.000000000000000000 ) ) ;
#21198=ADVANCED_FACE ( 'NONE', ( #33540 ), #66860, .F. ) ;
#21199=CARTESIAN_POINT ( 'NONE',  ( 15.18398860626900237, 28.73617430169797871, 5.000000000000000000 ) ) ;
#21200=EDGE_LOOP ( 'NONE', ( #57446, #99083, #134219, #63905 ) ) ;
#21201=EDGE_CURVE ( 'NONE', #134058, #90351, #119, .T. ) ;
#21202=ORIENTED_EDGE ( 'NONE', *, *, #5384, .T. ) ;
#21203=LINE ( 'NONE', #142980, #19426 ) ;
#21204=CARTESIAN_POINT ( 'NONE',  ( -36.29974487139159578, -27.71228299555231445, 4.000000000000000000 ) ) ;
#21205=VERTEX_POINT ( 'NONE', #44418 ) ;
#21206=EDGE_CURVE ( 'NONE', #69406, #73447, #57424, .T. ) ;
#21207=CARTESIAN_POINT ( 'NONE',  ( 24.29974487139158867, -27.71228299555223273, 4.000000000000000000 ) ) ;
#21209=DIRECTION ( 'NONE',  ( 0.6830127018922181881, 0.6830127018922202975, -0.2588190451025214056 ) ) ;
#21210=ORIENTED_EDGE ( 'NONE', *, *, #129093, .T. ) ;
#21211=ADVANCED_FACE ( 'NONE', ( #46582 ), #90767, .F. ) ;
#21212=DIRECTION ( 'NONE',  ( -0.000000000000000000, 0.000000000000000000, 1.000000000000000000 ) ) ;
#21213=DIRECTION ( 'NONE',  ( -0.6830127018922181881, 0.6830127018922202975, -0.2588190451025214056 ) ) ;
#21216=AXIS2_PLACEMENT_3D ( 'NONE', #53110, #31387, #75610 ) ;
#21219=CARTESIAN_POINT ( 'NONE',  ( -29.29289321881324426, -15.74070752338412760, 5.000000000000000000 ) ) ;
#21221=ORIENTED_EDGE ( 'NONE', *, *, #48712, .T. ) ;
#21222=ORIENTED_EDGE ( 'NONE', *, *, #116855, .T. ) ;
#21224=VECTOR ( 'NONE', #101391, 1000.000000000000227 ) ;
#21227=PLANE ( 'NONE',  #13147 ) ;
#21228=LINE ( 'NONE', #97326, #106317 ) ;
#21229=EDGE_CURVE ( 'NONE', #49159, #142584, #132850, .T. ) ;
#21230=ORIENTED_EDGE ( 'NONE', *, *, #134713, .T. ) ;
#21231=( BOUNDED_CURVE ( )  B_SPLINE_CURVE ( 3, ( #41719, #29402, #40321, #139642 ),
 .UNSPECIFIED., .F., .T. ) 
 B_SPLINE_CURVE_WITH_KNOTS ( ( 4, 4 ),
 ( 1.901594255663598299, 1.933014472006547635 ),
 .UNSPECIFIED. ) 
 CURVE ( )  GEOMETRIC_REPRESENTATION_ITEM ( )  RATIONAL_B_SPLINE_CURVE ( ( 1.000000000000000000, 0.9999177325257868620, 0.9999177325257868620, 1.000000000000000000 ) ) 
 REPRESENTATION_ITEM ( '' )  );
#21232=CARTESIAN_POINT ( 'NONE',  ( -2.700255128608413990, -27.71228299555204089, 4.000000000000000000 ) ) ;
#21233=CARTESIAN_POINT ( 'NONE',  ( -39.48921356237310221, -27.52281430457082934, 5.000000000000000000 ) ) ;
#21234=CARTESIAN_POINT ( 'NONE',  ( 5.901564193917593570, 11.25929247661560240, 10.79108189686408359 ) ) ;
#21235=LINE ( 'NONE', #40175, #3639 ) ;
#21236=ORIENTED_EDGE ( 'NONE', *, *, #23124, .T. ) ;
#21238=PLANE ( 'NONE',  #35271 ) ;
#21241=VECTOR ( 'NONE', #61725, 1000.000000000000000 ) ;
#21242=LINE ( 'NONE', #108937, #128906 ) ;
#21243=DIRECTION ( 'NONE',  ( 1.000000000000000000, 0.000000000000000000, 0.000000000000000000 ) ) ;
#21247=CARTESIAN_POINT ( 'NONE',  ( -31.49999999999978684, -20.94781430457059912, 5.000000000000000000 ) ) ;
#21248=CARTESIAN_POINT ( 'NONE',  ( 72.18398860626899705, 28.73617430169837661, 5.000000000000000000 ) ) ;
#21249=ORIENTED_EDGE ( 'NONE', *, *, #40569, .T. ) ;
#21250=VERTEX_POINT ( 'NONE', #130447 ) ;
#21252=DIRECTION ( 'NONE',  ( -0.000000000000000000, 0.000000000000000000, 1.000000000000000000 ) ) ;
#21253=PLANE ( 'NONE',  #73997 ) ;
#21256=ORIENTED_EDGE ( 'NONE', *, *, #107927, .F. ) ;
#21257=AXIS2_PLACEMENT_3D ( 'NONE', #123594, #24249, #88808 ) ;
#21259=CARTESIAN_POINT ( 'NONE',  ( 13.27644930412397350, 4.689949953678146599, 5.000000000000000000 ) ) ;
#21260=EDGE_CURVE ( 'NONE', #74923, #75266, #88372, .T. ) ;
#21262=EDGE_CURVE ( 'NONE', #132813, #53796, #20210, .T. ) ;
#21265=ORIENTED_EDGE ( 'NONE', *, *, #5808, .T. ) ;
#21266=ORIENTED_EDGE ( 'NONE', *, *, #47497, .F. ) ;
#21267=ORIENTED_EDGE ( 'NONE', *, *, #107012, .F. ) ;
#21268=VECTOR ( 'NONE', #112027, 1000.000000000000227 ) ;
#21269=VECTOR ( 'NONE', #70875, 1000.000000000000000 ) ;
#21272=LINE ( 'NONE', #11794, #110170 ) ;
#21273=DIRECTION ( 'NONE',  ( -0.7071067811865486830, 0.7071067811865464625, 0.000000000000000000 ) ) ;
#21274=CARTESIAN_POINT ( 'NONE',  ( 27.72281430457040940, -21.72500000000000142, 5.000000000000000000 ) ) ;
#21275=ORIENTED_EDGE ( 'NONE', *, *, #105529, .F. ) ;
#21277=PLANE ( 'NONE',  #26687 ) ;
#21278=CARTESIAN_POINT ( 'NONE',  ( 27.48921356237309155, -27.52281430457074762, 5.000000000000000000 ) ) ;
#21285=CARTESIAN_POINT ( 'NONE',  ( 14.24139925780194105, 21.72500000000000142, 5.000000000000000000 ) ) ;
#21286=CARTESIAN_POINT ( 'NONE',  ( -11.28769006033965461, -21.73547319004782352, 4.999917730833664642 ) ) ;
#21287=FACE_OUTER_BOUND ( 'NONE', #76635, .T. ) ;
#21288=EDGE_LOOP ( 'NONE', ( #59361, #93880, #143032, #29362 ) ) ;
#21290=LINE ( 'NONE', #54644, #47710 ) ;
#21292=CARTESIAN_POINT ( 'NONE',  ( 0.000000000000000000, 0.000000000000000000, 5.000000000000000000 ) ) ;
#21293=DIRECTION ( 'NONE',  ( 0.6830127018922181881, 0.6830127018922202975, -0.2588190451025214056 ) ) ;
#21294=CARTESIAN_POINT ( 'NONE',  ( -23.29298673570678702, -21.74070752338405299, 4.999753212805217117 ) ) ;
#21295=ORIENTED_EDGE ( 'NONE', *, *, #108774, .T. ) ;
#21296=ORIENTED_EDGE ( 'NONE', *, *, #70876, .T. ) ;
#21297=PLANE ( 'NONE',  #97900 ) ;
#21298=EDGE_CURVE ( 'NONE', #37141, #38602, #142734, .T. ) ;
#21299=VERTEX_POINT ( 'NONE', #109387 ) ;
#21300=VECTOR ( 'NONE', #5600, 1000.000000000000227 ) ;
#21301=VERTEX_POINT ( 'NONE', #32555 ) ;
#21303=DIRECTION ( 'NONE',  ( 0.3543493200069162685, -0.000000000000000000, -0.9351131265310288487 ) ) ;
#21305=VECTOR ( 'NONE', #44196, 1000.000000000000000 ) ;
#21306=DIRECTION ( 'NONE',  ( -0.6830127018922180770, -0.6830127018922204085, -0.2588190451025213501 ) ) ;
#21307=CARTESIAN_POINT ( 'NONE',  ( -11.99999999999990941, 17.96639925780208102, 5.000000000000000000 ) ) ;
#21308=AXIS2_PLACEMENT_3D ( 'NONE', #138216, #17829, #62100 ) ;
#21309=CARTESIAN_POINT ( 'NONE',  ( -13.43312800248734185, -21.74070752338406010, 6.915939825044106648 ) ) ;
#21310=FACE_BOUND ( 'NONE', #136050, .T. ) ;
#21311=DIRECTION ( 'NONE',  ( 0.6830127018922181881, 0.6830127018922202975, -0.2588190451025214056 ) ) ;
#21314=CARTESIAN_POINT ( 'NONE',  ( -11.29289321881337571, -15.74070752338412404, 5.000000000000000000 ) ) ;
#21317=FACE_OUTER_BOUND ( 'NONE', #24839, .T. ) ;
#21318=ORIENTED_EDGE ( 'NONE', *, *, #86028, .F. ) ;
#21322=EDGE_LOOP ( 'NONE', ( #56031, #56207, #113474, #107299 ) ) ;
#21323=DIRECTION ( 'NONE',  ( -0.7071067811865486830, -0.7071067811865464625, -0.000000000000000000 ) ) ;
#21324=DIRECTION ( 'NONE',  ( 0.000000000000000000, 1.000000000000000000, -0.000000000000000000 ) ) ;
#21325=VECTOR ( 'NONE', #138976, 1000.000000000000000 ) ;
#21326=VERTEX_POINT ( 'NONE', #65922 ) ;
#21327=DIRECTION ( 'NONE',  ( -0.7071067811865487940, 0.7071067811865463515, -0.000000000000000000 ) ) ;
#21328=AXIS2_PLACEMENT_3D ( 'NONE', #28189, #69581, #17299 ) ;
#21329=EDGE_CURVE ( 'NONE', #57666, #2587, #77508, .T. ) ;
#21331=LINE ( 'NONE', #76438, #78511 ) ;
#21333=DIRECTION ( 'NONE',  ( -0.7071067811865486830, -0.7071067811865464625, 0.000000000000000000 ) ) ;
#21334=CARTESIAN_POINT ( 'NONE',  ( 27.09667064187388874, -2.240707523384257716, 15.26439735382758833 ) ) ;
#21335=DIRECTION ( 'NONE',  ( -0.3543493200069162685, -0.000000000000000000, -0.9351131265310288487 ) ) ;
#21336=CARTESIAN_POINT ( 'NONE',  ( -34.92500000000001137, 14.81665438641027777, 4.500000000000000888 ) ) ;
#21337=ORIENTED_EDGE ( 'NONE', *, *, #74466, .F. ) ;
#21338=AXIS2_PLACEMENT_3D ( 'NONE', #93420, #60092, #59397 ) ;
#21340=ORIENTED_EDGE ( 'NONE', *, *, #87704, .F. ) ;
#21341=DIRECTION ( 'NONE',  ( 0.7071067811865487940, -0.7071067811865463515, 0.000000000000000000 ) ) ;
#21343=VERTEX_POINT ( 'NONE', #63064 ) ;
#21346=VECTOR ( 'NONE', #133400, 1000.000000000000227 ) ;
#21347=ORIENTED_EDGE ( 'NONE', *, *, #113697, .T. ) ;
#21348=FACE_OUTER_BOUND ( 'NONE', #11246, .T. ) ;
#21349=CARTESIAN_POINT ( 'NONE',  ( -56.99451991528749062, 28.92564299267978001, 4.000000000000000000 ) ) ;
#21352=EDGE_LOOP ( 'NONE', ( #88651, #26838, #93729, #126775 ) ) ;
#21354=EDGE_LOOP ( 'NONE', ( #3642, #100845, #40949, #41734 ) ) ;
#21355=PLANE ( 'NONE',  #85837 ) ;
#21356=LINE ( 'NONE', #98210, #114626 ) ;
#21357=AXIS2_PLACEMENT_3D ( 'NONE', #39418, #69936, #38693 ) ;
#21358=VECTOR ( 'NONE', #111212, 1000.000000000000000 ) ;
#21359=CARTESIAN_POINT ( 'NONE',  ( 1.828169399223519953, 15.75929247661555443, 4.000000000000000000 ) ) ;
#21360=ORIENTED_EDGE ( 'NONE', *, *, #51785, .F. ) ;
#21361=VECTOR ( 'NONE', #134729, 1000.000000000000227 ) ;
#21362=ORIENTED_EDGE ( 'NONE', *, *, #11552, .T. ) ;
#21364=LINE ( 'NONE', #133700, #67765 ) ;
#21365=VECTOR ( 'NONE', #112650, 1000.000000000000227 ) ;
#21366=CARTESIAN_POINT ( 'NONE',  ( -24.98911971346034377, -22.02621442084248216, 4.990779571109220214 ) ) ;
#21367=VECTOR ( 'NONE', #110096, 999.9999999999998863 ) ;
#21368=ORIENTED_EDGE ( 'NONE', *, *, #15378, .T. ) ;
#21370=ORIENTED_EDGE ( 'NONE', *, *, #114039, .F. ) ;
#21371=VERTEX_POINT ( 'NONE', #89853 ) ;
#21372=DIRECTION ( 'NONE',  ( -0.7071067811865487940, 0.7071067811865463515, 0.000000000000000000 ) ) ;
#21373=CARTESIAN_POINT ( 'NONE',  ( -19.49999999999987210, -4.216083040037264418, -7.486842126848610945 ) ) ;
#21375=FACE_OUTER_BOUND ( 'NONE', #49474, .T. ) ;
#21376=LINE ( 'NONE', #133019, #132684 ) ;
#21378=EDGE_CURVE ( 'NONE', #118711, #8834, #57271, .T. ) ;
#21379=DIRECTION ( 'NONE',  ( -0.7071067811865486830, 0.7071067811865464625, 0.000000000000000000 ) ) ;
#21380=CARTESIAN_POINT ( 'NONE',  ( -0.4892135623730947680, -27.52281430457055578, 5.000000000000000000 ) ) ;
#21382=EDGE_CURVE ( 'NONE', #122903, #96758, #136217, .T. ) ;
#21383=EDGE_LOOP ( 'NONE', ( #33975, #5445, #115443, #2240 ) ) ;
#21384=LINE ( 'NONE', #65644, #99880 ) ;
#21385=ORIENTED_EDGE ( 'NONE', *, *, #81843, .T. ) ;
#21386=DIRECTION ( 'NONE',  ( -0.7071067811865487940, 0.7071067811865463515, -0.000000000000000000 ) ) ;
#21387=EDGE_CURVE ( 'NONE', #50737, #78330, #45684, .T. ) ;
#21388=EDGE_CURVE ( 'NONE', #30943, #71410, #67429, .T. ) ;
#21389=DIRECTION ( 'NONE',  ( -0.6830127018922181881, 0.6830127018922202975, -0.2588190451025214056 ) ) ;
#21390=LINE ( 'NONE', #67039, #20692 ) ;
#21391=ORIENTED_EDGE ( 'NONE', *, *, #15540, .F. ) ;
#21392=LINE ( 'NONE', #119249, #36793 ) ;
#21393=PLANE ( 'NONE',  #118209 ) ;
#21394=CARTESIAN_POINT ( 'NONE',  ( -17.99451991528748351, 28.92564299267950645, 4.000000000000000000 ) ) ;
#21395=ORIENTED_EDGE ( 'NONE', *, *, #59320, .T. ) ;
#21396=ORIENTED_EDGE ( 'NONE', *, *, #111910, .F. ) ;
#21397=EDGE_CURVE ( 'NONE', #28705, #87694, #134099, .T. ) ;
#21399=DIRECTION ( 'NONE',  ( -0.7071067811865487940, 0.7071067811865463515, 0.000000000000000000 ) ) ;
#21400=DIRECTION ( 'NONE',  ( -0.7071067811865487940, 0.7071067811865463515, -0.000000000000000000 ) ) ;
#21401=DIRECTION ( 'NONE',  ( 1.000000000000000000, 0.000000000000000000, 0.000000000000000000 ) ) ;
#21403=DIRECTION ( 'NONE',  ( 0.7071067811865487940, 0.7071067811865463515, 0.000000000000000000 ) ) ;
#21404=EDGE_CURVE ( 'NONE', #53303, #117033, #1396, .T. ) ;
#21406=DIRECTION ( 'NONE',  ( -0.7071067811865486830, 0.7071067811865464625, 0.000000000000000000 ) ) ;
#21407=CARTESIAN_POINT ( 'NONE',  ( 15.48921356237309510, -27.52281430457066236, 5.000000000000000000 ) ) ;
#21409=EDGE_LOOP ( 'NONE', ( #36254, #48829, #9129, #64542 ) ) ;
#21410=DIRECTION ( 'NONE',  ( -0.7071067811865486830, -0.7071067811865464625, -0.000000000000000000 ) ) ;
#21411=ORIENTED_EDGE ( 'NONE', *, *, #93165, .T. ) ;
#21412=PLANE ( 'NONE',  #47780 ) ;
#21414=AXIS2_PLACEMENT_3D ( 'NONE', #103609, #36253, #49291 ) ;
#21415=CARTESIAN_POINT ( 'NONE',  ( 32.20710678118632586, 15.75929247661555443, 5.000000000000000000 ) ) ;
#21416=FACE_OUTER_BOUND ( 'NONE', #101919, .T. ) ;
#21418=LINE ( 'NONE', #64930, #99560 ) ;
#21419=LINE ( 'NONE', #19272, #63470 ) ;
#21420=VERTEX_POINT ( 'NONE', #124634 ) ;
#21421=EDGE_LOOP ( 'NONE', ( #52426, #103842, #90041, #24127, #20972 ) ) ;
#21422=PLANE ( 'NONE',  #71827 ) ;
#21425=EDGE_CURVE ( 'NONE', #94597, #108664, #90594, .T. ) ;
#21426=DIRECTION ( 'NONE',  ( 0.7071067811865487940, 0.7071067811865463515, 0.000000000000000000 ) ) ;
#21429=DIRECTION ( 'NONE',  ( 0.3543493200069162685, -0.000000000000000000, -0.9351131265310288487 ) ) ;
#21430=LINE ( 'NONE', #30146, #57661 ) ;
#21433=LINE ( 'NONE', #76545, #118689 ) ;
#21434=FACE_OUTER_BOUND ( 'NONE', #46842, .T. ) ;
#21435=PLANE ( 'NONE',  #102962 ) ;
#21436=ADVANCED_FACE ( 'NONE', ( #36902 ), #68858, .F. ) ;
#21438=ORIENTED_EDGE ( 'NONE', *, *, #23323, .T. ) ;
#21439=DIRECTION ( 'NONE',  ( -0.7071067811865486830, -0.7071067811865464625, 0.000000000000000000 ) ) ;
#21440=EDGE_CURVE ( 'NONE', #127258, #127118, #92705, .T. ) ;
#21441=ORIENTED_EDGE ( 'NONE', *, *, #72946, .F. ) ;
#21444=ORIENTED_EDGE ( 'NONE', *, *, #87858, .F. ) ;
#21445=AXIS2_PLACEMENT_3D ( 'NONE', #62308, #106467, #63039 ) ;
#21446=FACE_OUTER_BOUND ( 'NONE', #28992, .T. ) ;
#21447=EDGE_CURVE ( 'NONE', #2711, #41375, #58730, .T. ) ;
#21448=DIRECTION ( 'NONE',  ( 0.7071067811865486830, -0.7071067811865464625, -0.000000000000000000 ) ) ;
#21449=CARTESIAN_POINT ( 'NONE',  ( -7.499999999999958256, 16.08746187583909659, 4.000000000000000000 ) ) ;
#21452=CARTESIAN_POINT ( 'NONE',  ( -23.51078643762690490, -27.52281430457038880, 5.000000000000000000 ) ) ;
#21454=CARTESIAN_POINT ( 'NONE',  ( 6.938893903907228378E-15, -19.44781430457063465, 5.000000000000000000 ) ) ;
#21455=CARTESIAN_POINT ( 'NONE',  ( -57.18398860626899705, 28.73617430169827358, 5.000000000000000000 ) ) ;
#21458=DIRECTION ( 'NONE',  ( 0.000000000000000000, 0.000000000000000000, -1.000000000000000000 ) ) ;
#21459=EDGE_LOOP ( 'NONE', ( #133198, #15452, #128475, #84842, #26231 ) ) ;
#21460=ORIENTED_EDGE ( 'NONE', *, *, #50499, .T. ) ;
#21462=ORIENTED_EDGE ( 'NONE', *, *, #124486, .F. ) ;
#21463=EDGE_CURVE ( 'NONE', #39863, #5780, #12295, .T. ) ;
#21464=LINE ( 'NONE', #117869, #54514 ) ;
#21465=DIRECTION ( 'NONE',  ( -0.6830127018922180770, -0.6830127018922204085, -0.2588190451025213501 ) ) ;
#21469=ORIENTED_EDGE ( 'NONE', *, *, #117723, .F. ) ;
#21470=AXIS2_PLACEMENT_3D ( 'NONE', #120469, #78447, #21195 ) ;
#21471=AXIS2_PLACEMENT_3D ( 'NONE', #114018, #80006, #35059 ) ;
#21472=DIRECTION ( 'NONE',  ( -0.000000000000000000, 0.3543493200069153248, 0.9351131265310292928 ) ) ;
#21473=CARTESIAN_POINT ( 'NONE',  ( -27.18398860626900060, 28.73617430169806042, 5.000000000000000000 ) ) ;
#21474=VECTOR ( 'NONE', #94287, 1000.000000000000000 ) ;
#21477=DIRECTION ( 'NONE',  ( -0.6830127018922181881, 0.6830127018922202975, -0.2588190451025214056 ) ) ;
#21479=CARTESIAN_POINT ( 'NONE',  ( 51.18398860626899705, 28.73617430169823095, 5.000000000000000000 ) ) ;
#21480=CARTESIAN_POINT ( 'NONE',  ( -2.292893218813435219, -3.740707523384248390, 5.000000000000000000 ) ) ;
#21483=ORIENTED_EDGE ( 'NONE', *, *, #109193, .T. ) ;
#21484=EDGE_CURVE ( 'NONE', #15691, #6909, #15134, .T. ) ;
#21485=DIRECTION ( 'NONE',  ( -0.7071067811865486830, 0.7071067811865464625, 0.000000000000000000 ) ) ;
#21486=LINE ( 'NONE', #140398, #89456 ) ;
#21487=EDGE_CURVE ( 'NONE', #36751, #117439, #13702, .T. ) ;
#21490=DIRECTION ( 'NONE',  ( -0.6830127018922181881, 0.6830127018922202975, -0.2588190451025214056 ) ) ;
#21493=EDGE_LOOP ( 'NONE', ( #25423, #69122, #98367, #55278 ) ) ;
#21494=ADVANCED_FACE ( 'NONE', ( #135530 ), #125359, .T. ) ;
#21495=VECTOR ( 'NONE', #128559, 1000.000000000000000 ) ;
#21498=ORIENTED_EDGE ( 'NONE', *, *, #122931, .F. ) ;
#21499=VERTEX_POINT ( 'NONE', #59416 ) ;
#21501=EDGE_CURVE ( 'NONE', #132203, #60612, #102898, .T. ) ;
#21502=PLANE ( 'NONE',  #47810 ) ;
#21503=DIRECTION ( 'NONE',  ( 0.7071067811865486830, -0.7071067811865464625, -0.000000000000000000 ) ) ;
#21505=ORIENTED_EDGE ( 'NONE', *, *, #92284, .T. ) ;
#21506=DIRECTION ( 'NONE',  ( 1.000000000000000000, 0.000000000000000000, 0.000000000000000000 ) ) ;
#21508=LINE ( 'NONE', #1147, #98920 ) ;
#21509=DIRECTION ( 'NONE',  ( -0.000000000000000000, 0.000000000000000000, 1.000000000000000000 ) ) ;
#21510=DIRECTION ( 'NONE',  ( -0.6830127018922181881, 0.6830127018922202975, -0.2588190451025214056 ) ) ;
#21511=VECTOR ( 'NONE', #51242, 1000.000000000000000 ) ;
#21512=DIRECTION ( 'NONE',  ( -0.7071067811865487940, 0.7071067811865463515, -0.000000000000000000 ) ) ;
#21513=ORIENTED_EDGE ( 'NONE', *, *, #67389, .T. ) ;
#21514=PLANE ( 'NONE',  #68094 ) ;
#21515=FACE_OUTER_BOUND ( 'NONE', #132649, .T. ) ;
#21516=ORIENTED_EDGE ( 'NONE', *, *, #87459, .F. ) ;
#21517=ORIENTED_EDGE ( 'NONE', *, *, #77123, .F. ) ;
#21518=ADVANCED_FACE ( 'NONE', ( #8351 ), #75109, .F. ) ;
#21519=ORIENTED_EDGE ( 'NONE', *, *, #129201, .T. ) ;
#21521=ORIENTED_EDGE ( 'NONE', *, *, #19927, .F. ) ;
#21522=VECTOR ( 'NONE', #2089, 1000.000000000000227 ) ;
#21523=CARTESIAN_POINT ( 'NONE',  ( 18.18398860626898994, 28.73617430169800002, 5.000000000000000000 ) ) ;
#21526=DIRECTION ( 'NONE',  ( -0.7071067811865487940, 0.7071067811865463515, 0.000000000000000000 ) ) ;
#21527=VECTOR ( 'NONE', #90307, 1000.000000000000000 ) ;
#21528=ORIENTED_EDGE ( 'NONE', *, *, #66758, .F. ) ;
#21529=CARTESIAN_POINT ( 'NONE',  ( -23.29289321881329400, 11.25929247661559707, 5.000000000000000000 ) ) ;
#21531=LINE ( 'NONE', #65794, #70288 ) ;
#21534=VERTEX_POINT ( 'NONE', #30132 ) ;
#21536=ORIENTED_EDGE ( 'NONE', *, *, #54325, .F. ) ;
#21537=VERTEX_POINT ( 'NONE', #49247 ) ;
#21538=ORIENTED_EDGE ( 'NONE', *, *, #67424, .T. ) ;
#21540=AXIS2_PLACEMENT_3D ( 'NONE', #41802, #52662, #44705 ) ;
#21541=ORIENTED_EDGE ( 'NONE', *, *, #31406, .T. ) ;
#21542=EDGE_CURVE ( 'NONE', #23904, #47125, #9049, .T. ) ;
#21543=PLANE ( 'NONE',  #28345 ) ;
#21544=LINE ( 'NONE', #20090, #18539 ) ;
#21545=ADVANCED_FACE ( 'NONE', ( #85954 ), #93440, .T. ) ;
#21547=DIRECTION ( 'NONE',  ( 1.000000000000000000, 0.000000000000000000, 0.000000000000000000 ) ) ;
#21548=VECTOR ( 'NONE', #102763, 1000.000000000000000 ) ;
#21551=EDGE_CURVE ( 'NONE', #19553, #75708, #30880, .T. ) ;
#21553=CARTESIAN_POINT ( 'NONE',  ( 29.99999999999979394, 1.552185695429152856, 5.000000000000000000 ) ) ;
#21554=ADVANCED_FACE ( 'NONE', ( #64929 ), #97531, .T. ) ;
#21556=DIRECTION ( 'NONE',  ( -0.000000000000000000, -0.3543493200069152693, 0.9351131265310292928 ) ) ;
#21557=VERTEX_POINT ( 'NONE', #130912 ) ;
#21558=EDGE_LOOP ( 'NONE', ( #124030, #4507, #62677, #21817 ) ) ;
#21559=ADVANCED_FACE ( 'NONE', ( #81889 ), #19270, .F. ) ;
#21560=ORIENTED_EDGE ( 'NONE', *, *, #53348, .F. ) ;
#21561=DIRECTION ( 'NONE',  ( -0.6830127018922180770, -0.6830127018922204085, -0.2588190451025213501 ) ) ;
#21562=CARTESIAN_POINT ( 'NONE',  ( -15.18398860626900237, 28.73617430169797871, 5.000000000000000000 ) ) ;
#21565=ADVANCED_FACE ( 'NONE', ( #86684 ), #53312, .F. ) ;
#21566=DIRECTION ( 'NONE',  ( 0.7071067811865487940, 0.7071067811865463515, 0.000000000000000000 ) ) ;
#21567=CARTESIAN_POINT ( 'NONE',  ( -22.49999999999984368, 22.01701374228153085, 2.453858888625680468 ) ) ;
#21570=DIRECTION ( 'NONE',  ( 0.3543493200069162685, -0.000000000000000000, -0.9351131265310288487 ) ) ;
#21572=CARTESIAN_POINT ( 'NONE',  ( -28.49999999999979394, -20.94781430457060623, 5.000000000000000000 ) ) ;
#21574=ORIENTED_EDGE ( 'NONE', *, *, #37815, .F. ) ;
#21576=VECTOR ( 'NONE', #62486, 1000.000000000000000 ) ;
#21577=ORIENTED_EDGE ( 'NONE', *, *, #135256, .T. ) ;
#21579=VERTEX_POINT ( 'NONE', #4947 ) ;
#21580=EDGE_CURVE ( 'NONE', #123992, #38637, #115865, .T. ) ;
#21582=LINE ( 'NONE', #33895, #127435 ) ;
#21583=ORIENTED_EDGE ( 'NONE', *, *, #20914, .T. ) ;
#21584=CARTESIAN_POINT ( 'NONE',  ( 23.14818355038130449, 17.25929247661554200, 8.802941693769255949 ) ) ;
#21585=ORIENTED_EDGE ( 'NONE', *, *, #45221, .T. ) ;
#21586=LINE ( 'NONE', #123771, #117904 ) ;
#21587=VECTOR ( 'NONE', #66729, 1000.000000000000000 ) ;
#21588=ORIENTED_EDGE ( 'NONE', *, *, #20429, .F. ) ;
#21589=DIRECTION ( 'NONE',  ( 0.7071067811865487940, -0.7071067811865463515, 0.000000000000000000 ) ) ;
#21590=ORIENTED_EDGE ( 'NONE', *, *, #127346, .F. ) ;
#21592=LINE ( 'NONE', #88283, #26764 ) ;
#21594=DIRECTION ( 'NONE',  ( 0.3543493200069162685, -0.000000000000000000, -0.9351131265310288487 ) ) ;
#21595=CARTESIAN_POINT ( 'NONE',  ( 11.67183060077639212, -3.740707523384244837, 4.000000000000000000 ) ) ;
#21596=DIRECTION ( 'NONE',  ( -0.000000000000000000, 0.3543493200069153248, 0.9351131265310292928 ) ) ;
#21598=CARTESIAN_POINT ( 'NONE',  ( 34.42499999999998295, -13.45860074219782021, 5.000000000000000000 ) ) ;
#21601=PLANE ( 'NONE',  #25851 ) ;
#21602=LINE ( 'NONE', #109317, #140412 ) ;
#21603=ORIENTED_EDGE ( 'NONE', *, *, #11465, .F. ) ;
#21604=VECTOR ( 'NONE', #15593, 999.9999999999998863 ) ;
#21605=ORIENTED_EDGE ( 'NONE', *, *, #120403, .T. ) ;
#21606=CARTESIAN_POINT ( 'NONE',  ( 32.29289321881323360, -18.74070752338408852, 5.000000000000000000 ) ) ;
#21608=ADVANCED_FACE ( 'NONE', ( #42482 ), #94130, .F. ) ;
#21609=CARTESIAN_POINT ( 'NONE',  ( -34.49999999999975842, 4.464255608400450548, 4.994342998332166772 ) ) ;
#21613=VERTEX_POINT ( 'NONE', #143187 ) ;
#21615=PLANE ( 'NONE',  #122847 ) ;
#21616=EDGE_CURVE ( 'NONE', #71286, #21885, #122131, .T. ) ;
#21617=VECTOR ( 'NONE', #123581, 1000.000000000000000 ) ;
#21618=DIRECTION ( 'NONE',  ( 0.7071067811865487940, -0.7071067811865463515, 0.000000000000000000 ) ) ;
#21620=CARTESIAN_POINT ( 'NONE',  ( 23.99999999999983302, -1.068876922607798985, 4.000000000000000000 ) ) ;
#21622=ORIENTED_EDGE ( 'NONE', *, *, #98791, .T. ) ;
#21623=DIRECTION ( 'NONE',  ( -0.7071067811865487940, 0.7071067811865463515, 0.000000000000000000 ) ) ;
#21627=EDGE_CURVE ( 'NONE', #120820, #22844, #77256, .T. ) ;
#21628=DIRECTION ( 'NONE',  ( 1.000000000000000000, 0.000000000000000000, 0.000000000000000000 ) ) ;
#21629=VECTOR ( 'NONE', #21503, 1000.000000000000000 ) ;
#21630=ORIENTED_EDGE ( 'NONE', *, *, #54, .F. ) ;
#21631=ORIENTED_EDGE ( 'NONE', *, *, #9012, .T. ) ;
#21632=EDGE_LOOP ( 'NONE', ( #54011, #42210, #52675, #41104 ) ) ;
#21635=VERTEX_POINT ( 'NONE', #46044 ) ;
#21636=EDGE_CURVE ( 'NONE', #22385, #44324, #101098, .T. ) ;
#21638=VECTOR ( 'NONE', #91623, 1000.000000000000000 ) ;
#21641=PLANE ( 'NONE',  #79215 ) ;
#21642=CARTESIAN_POINT ( 'NONE',  ( 13.49999999999990763, -7.533600742197660516, 5.000000000000000000 ) ) ;
#21643=( BOUNDED_CURVE ( )  B_SPLINE_CURVE ( 3, ( #68238, #112412, #35604, #69647 ),
 .UNSPECIFIED., .F., .F. ) 
 B_SPLINE_CURVE_WITH_KNOTS ( ( 4, 4 ),
 ( 1.901594255663624056, 1.933014472006568507 ),
 .UNSPECIFIED. ) 
 CURVE ( )  GEOMETRIC_REPRESENTATION_ITEM ( )  RATIONAL_B_SPLINE_CURVE ( ( 1.000000000000000000, 0.9999177325257868620, 0.9999177325257868620, 1.000000000000000000 ) ) 
 REPRESENTATION_ITEM ( '' )  );
#21645=VERTEX_POINT ( 'NONE', #100409 ) ;
#21646=CARTESIAN_POINT ( 'NONE',  ( -2.999999999999981792, -13.06887692260768219, 4.000000000000000000 ) ) ;
#21649=VERTEX_POINT ( 'NONE', #76528 ) ;
#21650=ORIENTED_EDGE ( 'NONE', *, *, #45372, .T. ) ;
#21651=EDGE_CURVE ( 'NONE', #18367, #96125, #87392, .T. ) ;
#21652=EDGE_LOOP ( 'NONE', ( #99402, #123924, #42432, #131398 ) ) ;
#21653=LINE ( 'NONE', #9291, #67659 ) ;
#21654=ADVANCED_FACE ( 'NONE', ( #120703 ), #342, .F. ) ;
#21655=CARTESIAN_POINT ( 'NONE',  ( 4.499999999999975131, 18.05218569542898521, 5.000000000000000000 ) ) ;
#21658=VECTOR ( 'NONE', #54809, 1000.000000000000227 ) ;
#21659=LINE ( 'NONE', #73382, #16362 ) ;
#21661=CARTESIAN_POINT ( 'NONE',  ( 34.49999999999975842, -8.568876922607724822, 4.000000000000000000 ) ) ;
#21662=AXIS2_PLACEMENT_3D ( 'NONE', #47598, #99784, #14199 ) ;
#21663=ORIENTED_EDGE ( 'NONE', *, *, #92408, .T. ) ;
#21664=ORIENTED_EDGE ( 'NONE', *, *, #90851, .T. ) ;
#21665=CARTESIAN_POINT ( 'NONE',  ( 13.36246187583893530, 22.22500000000000142, 4.000000000000000000 ) ) ;
#21666=ORIENTED_EDGE ( 'NONE', *, *, #102887, .T. ) ;
#21668=VECTOR ( 'NONE', #47744, 999.9999999999998863 ) ;
#21669=LINE ( 'NONE', #87634, #123784 ) ;
#21670=EDGE_CURVE ( 'NONE', #64780, #100429, #54769, .T. ) ;
#21671=ORIENTED_EDGE ( 'NONE', *, *, #102837, .F. ) ;
#21672=DIRECTION ( 'NONE',  ( 0.7071067811865487940, 0.7071067811865463515, -0.000000000000000000 ) ) ;
#21674=ORIENTED_EDGE ( 'NONE', *, *, #4276, .F. ) ;
#21676=CARTESIAN_POINT ( 'NONE',  ( -28.49999999999980460, 21.43112307739196254, 4.000000000000000000 ) ) ;
#21679=VERTEX_POINT ( 'NONE', #45341 ) ;
#21680=CARTESIAN_POINT ( 'NONE',  ( 14.99999999999989875, -10.06887692260770528, 4.000000000000000000 ) ) ;
#21681=VERTEX_POINT ( 'NONE', #22103 ) ;
#21682=DIRECTION ( 'NONE',  ( -0.7071067811865487940, 0.7071067811865463515, -0.000000000000000000 ) ) ;
#21684=ORIENTED_EDGE ( 'NONE', *, *, #75596, .F. ) ;
#21685=LINE ( 'NONE', #65934, #82980 ) ;
#21686=ORIENTED_EDGE ( 'NONE', *, *, #60379, .T. ) ;
#21687=ORIENTED_EDGE ( 'NONE', *, *, #70708, .T. ) ;
#21689=ORIENTED_EDGE ( 'NONE', *, *, #15045, .T. ) ;
#21690=CARTESIAN_POINT ( 'NONE',  ( -34.92500000000001137, -22.22500000000000142, 4.000000000000000000 ) ) ;
#21691=DIRECTION ( 'NONE',  ( -0.000000000000000000, -0.3543493200069152693, 0.9351131265310292928 ) ) ;
#21692=PLANE ( 'NONE',  #100484 ) ;
#21693=PLANE ( 'NONE',  #29948 ) ;
#21694=CARTESIAN_POINT ( 'NONE',  ( 6.183988606268994381, 28.73617430169791476, 5.000000000000000000 ) ) ;
#21695=DIRECTION ( 'NONE',  ( -1.000000000000000000, 0.000000000000000000, 0.000000000000000000 ) ) ;
#21696=AXIS2_PLACEMENT_3D ( 'NONE', #13308, #135830, #36516 ) ;
#21697=CARTESIAN_POINT ( 'NONE',  ( 20.99999999999985789, 19.93112307739198386, 4.000000000000000000 ) ) ;
#21698=LINE ( 'NONE', #89798, #34362 ) ;
#21699=CARTESIAN_POINT ( 'NONE',  ( 39.48921356237310221, -27.52281430457082934, 5.000000000000000000 ) ) ;
#21701=FACE_OUTER_BOUND ( 'NONE', #125557, .T. ) ;
#21702=ORIENTED_EDGE ( 'NONE', *, *, #56322, .T. ) ;
#21703=ORIENTED_EDGE ( 'NONE', *, *, #112878, .F. ) ;
#21705=EDGE_LOOP ( 'NONE', ( #63345, #109426, #92467, #51491 ) ) ;
#21706=PLANE ( 'NONE',  #130503 ) ;
#21707=ORIENTED_EDGE ( 'NONE', *, *, #76936, .F. ) ;
#21708=VECTOR ( 'NONE', #73457, 1000.000000000000000 ) ;
#21709=ORIENTED_EDGE ( 'NONE', *, *, #75912, .F. ) ;
#21710=DIRECTION ( 'NONE',  ( 1.000000000000000000, 0.000000000000000000, 0.000000000000000000 ) ) ;
#21712=CARTESIAN_POINT ( 'NONE',  ( 27.48921356237309155, -27.52281430457074762, 5.000000000000000000 ) ) ;
#21713=PLANE ( 'NONE',  #64965 ) ;
#21714=ORIENTED_EDGE ( 'NONE', *, *, #17517, .T. ) ;
#21715=DIRECTION ( 'NONE',  ( 0.6830127018922181881, 0.6830127018922202975, -0.2588190451025214056 ) ) ;
#21716=ORIENTED_EDGE ( 'NONE', *, *, #30041, .T. ) ;
#21719=VECTOR ( 'NONE', #45958, 1000.000000000000000 ) ;
#21721=VECTOR ( 'NONE', #112985, 1000.000000000000000 ) ;
#21723=ORIENTED_EDGE ( 'NONE', *, *, #54023, .F. ) ;
#21725=EDGE_CURVE ( 'NONE', #1414, #50020, #78651, .T. ) ;
#21726=LINE ( 'NONE', #110832, #140778 ) ;
#21727=EDGE_CURVE ( 'NONE', #42250, #51263, #60491, .T. ) ;
#21729=DIRECTION ( 'NONE',  ( 1.000000000000000000, 0.000000000000000000, 0.000000000000000000 ) ) ;
#21730=ORIENTED_EDGE ( 'NONE', *, *, #15073, .F. ) ;
#21731=EDGE_LOOP ( 'NONE', ( #41878, #82099, #76205, #100617 ) ) ;
#21732=ADVANCED_FACE ( 'NONE', ( #26414 ), #113394, .F. ) ;
#21733=EDGE_LOOP ( 'NONE', ( #22645, #42380, #73517, #79170 ) ) ;
#21734=CARTESIAN_POINT ( 'NONE',  ( -16.49999999999988276, 5.696342897626497148, -7.587980461218440276 ) ) ;
#21735=CARTESIAN_POINT ( 'NONE',  ( -23.03315071937583980, 7.620612595215163765, 4.000000000000000000 ) ) ;
#21736=AXIS2_PLACEMENT_3D ( 'NONE', #12822, #122292, #11370 ) ;
#21737=DIRECTION ( 'NONE',  ( -0.7071067811865487940, 0.7071067811865463515, -0.000000000000000000 ) ) ;
#21738=CARTESIAN_POINT ( 'NONE',  ( 28.49999999999980105, 6.277155672890298632, -3.510561720659008067 ) ) ;
#21739=EDGE_CURVE ( 'NONE', #65454, #124871, #104669, .T. ) ;
#21740=CARTESIAN_POINT ( 'NONE',  ( 31.99806943317879515, -22.22500000000000142, 4.500000000000000888 ) ) ;
#21741=VERTEX_POINT ( 'NONE', #49622 ) ;
#21742=DIRECTION ( 'NONE',  ( 0.7071067811865486830, -0.7071067811865464625, -0.000000000000000000 ) ) ;
#21743=EDGE_CURVE ( 'NONE', #14566, #19705, #101822, .T. ) ;
#21744=DIRECTION ( 'NONE',  ( 0.3543493200069162685, -0.000000000000000000, -0.9351131265310288487 ) ) ;
#21745=VERTEX_POINT ( 'NONE', #14807 ) ;
#21746=CARTESIAN_POINT ( 'NONE',  ( -0.7928932188134494297, -11.24070752338417023, 5.000000000000000000 ) ) ;
#21747=VECTOR ( 'NONE', #20633, 1000.000000000000000 ) ;
#21748=DIRECTION ( 'NONE',  ( -0.7071067811865486830, -0.7071067811865464625, 0.000000000000000000 ) ) ;
#21749=ORIENTED_EDGE ( 'NONE', *, *, #67272, .T. ) ;
#21750=ADVANCED_FACE ( 'NONE', ( #4578 ), #93092, .F. ) ;
#21751=DIRECTION ( 'NONE',  ( -0.3543493200069162685, -0.000000000000000000, -0.9351131265310288487 ) ) ;
#21752=ORIENTED_EDGE ( 'NONE', *, *, #119900, .F. ) ;
#21753=ORIENTED_EDGE ( 'NONE', *, *, #11456, .F. ) ;
#21754=EDGE_CURVE ( 'NONE', #139296, #11674, #36559, .T. ) ;
#21755=DIRECTION ( 'NONE',  ( -0.7071067811865486830, 0.7071067811865464625, 0.000000000000000000 ) ) ;
#21756=FACE_OUTER_BOUND ( 'NONE', #40952, .T. ) ;
#21757=ORIENTED_EDGE ( 'NONE', *, *, #142328, .T. ) ;
#21758=CARTESIAN_POINT ( 'NONE',  ( -66.18398860626901126, 28.73617430169833753, 5.000000000000000000 ) ) ;
#21759=EDGE_CURVE ( 'NONE', #58827, #7365, #35888, .T. ) ;
#21760=LINE ( 'NONE', #41350, #140101 ) ;
#21762=VECTOR ( 'NONE', #22735, 999.9999999999998863 ) ;
#21763=CARTESIAN_POINT ( 'NONE',  ( 33.18398860626899705, 28.73617430169810305, 5.000000000000000000 ) ) ;
#21764=DIRECTION ( 'NONE',  ( 0.7071067811865487940, 0.7071067811865463515, 0.000000000000000000 ) ) ;
#21765=CARTESIAN_POINT ( 'NONE',  ( 5.999999999999963585, -0.8619312979531862373, -5.102805207349813799 ) ) ;
#21766=DIRECTION ( 'NONE',  ( -0.000000000000000000, 0.3543493200069153248, 0.9351131265310292928 ) ) ;
#21767=DIRECTION ( 'NONE',  ( 0.7071067811865486830, -0.7071067811865464625, -0.000000000000000000 ) ) ;
#21768=LINE ( 'NONE', #22446, #26006 ) ;
#21769=DIRECTION ( 'NONE',  ( -0.3543493200069162685, -0.000000000000000000, -0.9351131265310288487 ) ) ;
#21771=CARTESIAN_POINT ( 'NONE',  ( -23.60898926630779826, -0.6778661889157658882, 4.000000000000000000 ) ) ;
#21772=ORIENTED_EDGE ( 'NONE', *, *, #135022, .T. ) ;
#21773=VECTOR ( 'NONE', #70583, 1000.000000000000000 ) ;
#21774=EDGE_LOOP ( 'NONE', ( #2942, #28355, #66343, #39487 ) ) ;
#21776=EDGE_LOOP ( 'NONE', ( #4871, #141106, #80781, #92146 ) ) ;
#21777=ORIENTED_EDGE ( 'NONE', *, *, #84100, .T. ) ;
#21778=ORIENTED_EDGE ( 'NONE', *, *, #20363, .F. ) ;
#21779=ADVANCED_FACE ( 'NONE', ( #82240 ), #93798, .F. ) ;
#21780=CARTESIAN_POINT ( 'NONE',  ( 0.000000000000000000, 0.000000000000000000, 5.000000000000000000 ) ) ;
#21781=DIRECTION ( 'NONE',  ( 0.7071067811865487940, 0.7071067811865463515, 0.000000000000000000 ) ) ;
#21782=EDGE_LOOP ( 'NONE', ( #58327, #133156, #67797, #67499 ) ) ;
#21783=CARTESIAN_POINT ( 'NONE',  ( -22.49999999999984723, -4.216083040037270635, -7.486842126848605616 ) ) ;
#21784=DIRECTION ( 'NONE',  ( 0.7071067811865487940, -0.7071067811865463515, 0.000000000000000000 ) ) ;
#21785=LINE ( 'NONE', #31248, #108898 ) ;
#21786=CARTESIAN_POINT ( 'NONE',  ( 34.49999999999975842, -17.91344420646039381, 1.358650452708543233 ) ) ;
#21787=ORIENTED_EDGE ( 'NONE', *, *, #79210, .F. ) ;
#21788=CARTESIAN_POINT ( 'NONE',  ( 21.79289321881330821, -5.240707523384228850, 5.000000000000000000 ) ) ;
#21789=DIRECTION ( 'NONE',  ( -0.7071067811865487940, 0.7071067811865463515, -0.000000000000000000 ) ) ;
#21790=AXIS2_PLACEMENT_3D ( 'NONE', #110457, #90152, #123537 ) ;
#21791=LINE ( 'NONE', #70364, #77627 ) ;
#21792=FACE_OUTER_BOUND ( 'NONE', #71306, .T. ) ;
#21793=DIRECTION ( 'NONE',  ( 0.7071067811865487940, 0.7071067811865463515, 0.000000000000000000 ) ) ;
#21795=ADVANCED_FACE ( 'NONE', ( #16200 ), #138025, .F. ) ;
#21796=DIRECTION ( 'NONE',  ( 1.000000000000000000, 0.000000000000000000, 0.000000000000000000 ) ) ;
#21797=VECTOR ( 'NONE', #136769, 1000.000000000000227 ) ;
#21798=ORIENTED_EDGE ( 'NONE', *, *, #111751, .T. ) ;
#21799=ORIENTED_EDGE ( 'NONE', *, *, #11913, .F. ) ;
#21803=CARTESIAN_POINT ( 'NONE',  ( 34.49999999999975842, -16.53574439159934073, 4.994342998332164107 ) ) ;
#21804=EDGE_CURVE ( 'NONE', #10041, #21534, #127129, .T. ) ;
#21805=CARTESIAN_POINT ( 'NONE',  ( 21.48921356237309155, -27.52281430457070499, 5.000000000000000000 ) ) ;
#21806=CARTESIAN_POINT ( 'NONE',  ( 8.510786437626906675, -27.52281430457049183, 5.000000000000000000 ) ) ;
#21808=CARTESIAN_POINT ( 'NONE',  ( -6.299744871391586898, -27.71228299555210484, 4.000000000000000000 ) ) ;
#21810=VECTOR ( 'NONE', #112154, 1000.000000000000000 ) ;
#21811=ORIENTED_EDGE ( 'NONE', *, *, #83733, .F. ) ;
#21812=ADVANCED_FACE ( 'NONE', ( #82935 ), #48163, .F. ) ;
#21814=CARTESIAN_POINT ( 'NONE',  ( -3.299744871391591339, -27.71228299555208352, 4.000000000000000000 ) ) ;
#21815=DIRECTION ( 'NONE',  ( 1.000000000000000000, 0.000000000000000000, 0.000000000000000000 ) ) ;
#21816=ORIENTED_EDGE ( 'NONE', *, *, #71120, .T. ) ;
#21817=ORIENTED_EDGE ( 'NONE', *, *, #43951, .F. ) ;
#21819=AXIS2_PLACEMENT_3D ( 'NONE', #50966, #82890, #16904 ) ;
#21820=ADVANCED_FACE ( 'NONE', ( #116267 ), #2475, .F. ) ;
#21821=ORIENTED_EDGE ( 'NONE', *, *, #138060, .F. ) ;
#21822=FACE_OUTER_BOUND ( 'NONE', #46540, .T. ) ;
#21823=LINE ( 'NONE', #124527, #101067 ) ;
#21824=CARTESIAN_POINT ( 'NONE',  ( 21.48921356237309155, -27.52281430457070499, 5.000000000000000000 ) ) ;
#21825=( BOUNDED_CURVE ( )  B_SPLINE_CURVE ( 3, ( #48154, #37274, #138016, #114795 ),
 .UNSPECIFIED., .F., .T. ) 
 B_SPLINE_CURVE_WITH_KNOTS ( ( 4, 4 ),
 ( 5.005968288816736056, 5.074607125596337198 ),
 .UNSPECIFIED. ) 
 CURVE ( )  GEOMETRIC_REPRESENTATION_ITEM ( )  RATIONAL_B_SPLINE_CURVE ( ( 1.000000000000000000, 0.9996074310407765395, 0.9996074310407765395, 1.000000000000000000 ) ) 
 REPRESENTATION_ITEM ( '' )  );
#21827=VECTOR ( 'NONE', #90922, 1000.000000000000000 ) ;
#21829=ORIENTED_EDGE ( 'NONE', *, *, #142541, .T. ) ;
#21830=LINE ( 'NONE', #66073, #140494 ) ;
#21832=ORIENTED_EDGE ( 'NONE', *, *, #53790, .T. ) ;
#21834=FACE_OUTER_BOUND ( 'NONE', #113773, .T. ) ;
#21835=CARTESIAN_POINT ( 'NONE',  ( -75.18398860626899705, 28.73617430169839793, 5.000000000000000000 ) ) ;
#21836=EDGE_CURVE ( 'NONE', #92930, #49206, #58379, .T. ) ;
#21838=CARTESIAN_POINT ( 'NONE',  ( 6.005480084712508493, 28.92564299267933947, 4.000000000000000000 ) ) ;
#21839=DIRECTION ( 'NONE',  ( -0.7071067811865487940, 0.7071067811865463515, -0.000000000000000000 ) ) ;
#21840=EDGE_CURVE ( 'NONE', #61158, #45578, #47496, .T. ) ;
#21841=FACE_BOUND ( 'NONE', #70778, .T. ) ;
#21842=ORIENTED_EDGE ( 'NONE', *, *, #72843, .T. ) ;
#21845=ADVANCED_FACE ( 'NONE', ( #25679 ), #81533, .T. ) ;
#21846=ORIENTED_EDGE ( 'NONE', *, *, #25805, .T. ) ;
#21847=DIRECTION ( 'NONE',  ( -0.000000000000000000, 0.3543493200069153248, 0.9351131265310292928 ) ) ;
#21848=EDGE_LOOP ( 'NONE', ( #122430, #45087, #135707, #31509 ) ) ;
#21849=EDGE_LOOP ( 'NONE', ( #47298, #14742, #87058, #79685 ) ) ;
#21851=ORIENTED_EDGE ( 'NONE', *, *, #42537, .T. ) ;
#21853=ORIENTED_EDGE ( 'NONE', *, *, #52776, .T. ) ;
#21854=CARTESIAN_POINT ( 'NONE',  ( -72.18398860626899705, 28.73617430169837661, 5.000000000000000000 ) ) ;
#21855=DIRECTION ( 'NONE',  ( -0.7071067811865487940, 0.7071067811865463515, -0.000000000000000000 ) ) ;
#21856=FACE_OUTER_BOUND ( 'NONE', #105427, .T. ) ;
#21859=LINE ( 'NONE', #801, #115235 ) ;
#21860=EDGE_CURVE ( 'NONE', #111536, #103780, #19796, .T. ) ;
#21861=AXIS2_PLACEMENT_3D ( 'NONE', #110107, #53621, #54358 ) ;
#21863=CARTESIAN_POINT ( 'NONE',  ( 33.29974487139158867, -27.71228299555229313, 4.000000000000000000 ) ) ;
#21864=CARTESIAN_POINT ( 'NONE',  ( -45.18398860626900415, 28.73617430169818832, 5.000000000000000000 ) ) ;
#21865=CARTESIAN_POINT ( 'NONE',  ( -10.49999999999991296, 22.08746187583902199, 4.000000000000000000 ) ) ;
#21866=LINE ( 'NONE', #87134, #50988 ) ;
#21867=EDGE_LOOP ( 'NONE', ( #130970, #95805, #141935 ) ) ;
#21868=ORIENTED_EDGE ( 'NONE', *, *, #120092, .F. ) ;
#21869=VERTEX_POINT ( 'NONE', #86510 ) ;
#21870=LINE ( 'NONE', #110286, #128384 ) ;
#21871=CARTESIAN_POINT ( 'NONE',  ( 71.99451991528749772, 28.92564299267988304, 4.000000000000000000 ) ) ;
#21872=EDGE_LOOP ( 'NONE', ( #133447, #115737, #32936, #91347 ) ) ;
#21873=ORIENTED_EDGE ( 'NONE', *, *, #54268, .F. ) ;
#21875=DIRECTION ( 'NONE',  ( 0.000000000000000000, 0.000000000000000000, 1.000000000000000000 ) ) ;
#21876=LINE ( 'NONE', #110292, #67127 ) ;
#21878=FACE_OUTER_BOUND ( 'NONE', #92946, .T. ) ;
#21879=VECTOR ( 'NONE', #101024, 999.9999999999998863 ) ;
#21880=LINE ( 'NONE', #99419, #51381 ) ;
#21883=EDGE_CURVE ( 'NONE', #120012, #56830, #116971, .T. ) ;
#21884=CARTESIAN_POINT ( 'NONE',  ( 8.669897814527296021, 17.25929247661553845, 19.83885114516069237 ) ) ;
#21885=VERTEX_POINT ( 'NONE', #74197 ) ;
#21887=EDGE_CURVE ( 'NONE', #32991, #60304, #8862, .T. ) ;
#21888=AXIS2_PLACEMENT_3D ( 'NONE', #97343, #18349, #83681 ) ;
#21889=DIRECTION ( 'NONE',  ( 0.7071067811865487940, 0.7071067811865463515, 0.000000000000000000 ) ) ;
#21890=LINE ( 'NONE', #79898, #33450 ) ;
#21891=CARTESIAN_POINT ( 'NONE',  ( 69.29974487139159578, -27.71228299555254537, 4.000000000000000000 ) ) ;
#21892=ORIENTED_EDGE ( 'NONE', *, *, #85244, .T. ) ;
#21893=EDGE_LOOP ( 'NONE', ( #141497, #21684, #55337, #30469 ) ) ;
#21894=CARTESIAN_POINT ( 'NONE',  ( -8.999999999999944933, 20.58746187583905041, 4.000000000000000000 ) ) ;
#21895=LINE ( 'NONE', #840, #107128 ) ;
#21896=ADVANCED_FACE ( 'NONE', ( #130000 ), #51019, .F. ) ;
#21897=EDGE_CURVE ( 'NONE', #121709, #54552, #29246, .T. ) ;
#21899=ORIENTED_EDGE ( 'NONE', *, *, #75961, .T. ) ;
#21901=LINE ( 'NONE', #1543, #111282 ) ;
#21902=LINE ( 'NONE', #66150, #46853 ) ;
#21903=EDGE_LOOP ( 'NONE', ( #133136, #14746, #123489, #40478 ) ) ;
#21904=CARTESIAN_POINT ( 'NONE',  ( 65.99451991528749772, 28.92564299267984396, 4.000000000000000000 ) ) ;
#21905=FACE_OUTER_BOUND ( 'NONE', #79134, .T. ) ;
#21907=EDGE_CURVE ( 'NONE', #75102, #20507, #129265, .T. ) ;
#21911=EDGE_CURVE ( 'NONE', #109724, #38733, #85768, .T. ) ;
#21912=VERTEX_POINT ( 'NONE', #140850 ) ;
#21915=ORIENTED_EDGE ( 'NONE', *, *, #5476, .F. ) ;
#21916=EDGE_CURVE ( 'NONE', #138157, #13042, #130738, .T. ) ;
#21917=CARTESIAN_POINT ( 'NONE',  ( -3.489213562373097322, -27.52281430457057709, 5.000000000000000000 ) ) ;
#21918=VECTOR ( 'NONE', #125509, 1000.000000000000227 ) ;
#21919=VECTOR ( 'NONE', #28875, 1000.000000000000000 ) ;
#21920=CARTESIAN_POINT ( 'NONE',  ( -1.499999999999984901, -16.91253812416058722, 4.000000000000000000 ) ) ;
#21921=CARTESIAN_POINT ( 'NONE',  ( 42.48921356237308800, -27.52281430457085065, 5.000000000000000000 ) ) ;
#21922=VERTEX_POINT ( 'NONE', #6737 ) ;
#21923=CARTESIAN_POINT ( 'NONE',  ( 15.70612307739184565, 22.22500000000000142, 4.000000000000000000 ) ) ;
#21924=DIRECTION ( 'NONE',  ( 0.6830127018922180770, -0.6830127018922204085, -0.2588190451025213501 ) ) ;
#21925=ADVANCED_FACE ( 'NONE', ( #39443 ), #61911, .F. ) ;
#21926=LINE ( 'NONE', #98073, #8852 ) ;
#21928=CARTESIAN_POINT ( 'NONE',  ( 17.99999999999987566, -21.41253812416053748, 4.000000000000000000 ) ) ;
#21930=ORIENTED_EDGE ( 'NONE', *, *, #129621, .T. ) ;
#21933=ORIENTED_EDGE ( 'NONE', *, *, #913, .T. ) ;
#21934=EDGE_CURVE ( 'NONE', #48771, #27746, #97332, .T. ) ;
#21935=CARTESIAN_POINT ( 'NONE',  ( 34.92499999999998295, 22.22500000000000142, 4.000000000000000000 ) ) ;
#21936=DIRECTION ( 'NONE',  ( -0.6830127018922180770, -0.6830127018922204085, -0.2588190451025213501 ) ) ;
#21937=EDGE_LOOP ( 'NONE', ( #81963, #142145, #58983, #65040 ) ) ;
#21938=LINE ( 'NONE', #133577, #115640 ) ;
#21939=CARTESIAN_POINT ( 'NONE',  ( 23.67183060077630330, 20.25929247661551003, 4.000000000000000000 ) ) ;
#21940=CARTESIAN_POINT ( 'NONE',  ( -8.671830600776413434, -15.74070752338412404, 4.000000000000000000 ) ) ;
#21943=VERTEX_POINT ( 'NONE', #140171 ) ;
#21944=EDGE_CURVE ( 'NONE', #45954, #60787, #75629, .T. ) ;
#21945=DIRECTION ( 'NONE',  ( 0.7071067811865487940, 0.7071067811865463515, -0.000000000000000000 ) ) ;
#21946=FACE_OUTER_BOUND ( 'NONE', #37669, .T. ) ;
#21947=EDGE_CURVE ( 'NONE', #124891, #98488, #105375, .T. ) ;
#21949=CARTESIAN_POINT ( 'NONE',  ( 5.207106781186511490, -14.24070752338413648, 5.000000000000000000 ) ) ;
#21950=DIRECTION ( 'NONE',  ( -0.7071067811865486830, -0.7071067811865464625, -0.000000000000000000 ) ) ;
#21952=CARTESIAN_POINT ( 'NONE',  ( -19.17183060077633883, -14.24070752338413648, 4.000000000000000000 ) ) ;
#21954=ADVANCED_FACE ( 'NONE', ( #74934 ), #72819, .T. ) ;
#21955=CARTESIAN_POINT ( 'NONE',  ( 3.183988606268992161, 28.73617430169789699, 5.000000000000000000 ) ) ;
#21956=DIRECTION ( 'NONE',  ( -0.7071067811865486830, 0.7071067811865464625, 0.000000000000000000 ) ) ;
#21957=ORIENTED_EDGE ( 'NONE', *, *, #113042, .T. ) ;
#21958=ORIENTED_EDGE ( 'NONE', *, *, #121016, .T. ) ;
#21961=LINE ( 'NONE', #66207, #129518 ) ;
#21963=CARTESIAN_POINT ( 'NONE',  ( 34.82816939922328459, 3.759292476615678336, 4.000000000000000000 ) ) ;
#21965=LINE ( 'NONE', #88680, #42189 ) ;
#21967=ORIENTED_EDGE ( 'NONE', *, *, #50144, .T. ) ;
#21968=ORIENTED_EDGE ( 'NONE', *, *, #130750, .F. ) ;
#21969=ORIENTED_EDGE ( 'NONE', *, *, #100100, .F. ) ;
#21970=FACE_OUTER_BOUND ( 'NONE', #75342, .T. ) ;
#21971=CARTESIAN_POINT ( 'NONE',  ( -34.92500000000001137, 21.72500000000000142, 5.000000000000000000 ) ) ;
#21972=DIRECTION ( 'NONE',  ( 0.7071067811865487940, 0.7071067811865463515, 0.000000000000000000 ) ) ;
#21973=LINE ( 'NONE', #66221, #55672 ) ;
#21974=VERTEX_POINT ( 'NONE', #6032 ) ;
#21975=CARTESIAN_POINT ( 'NONE',  ( -28.17183060077628198, 12.75929247661558286, 4.000000000000000000 ) ) ;
#21976=DIRECTION ( 'NONE',  ( -0.000000000000000000, 0.000000000000000000, 1.000000000000000000 ) ) ;
#21977=ORIENTED_EDGE ( 'NONE', *, *, #33830, .F. ) ;
#21980=DIRECTION ( 'NONE',  ( 0.6830127018922180770, -0.6830127018922204085, -0.2588190451025213501 ) ) ;
#21981=CARTESIAN_POINT ( 'NONE',  ( 23.29320749275911595, 20.25929247661551358, 20.83292124670809642 ) ) ;
#21982=CARTESIAN_POINT ( 'NONE',  ( 34.75611968250419181, 19.70565069852384354, 4.955485411084880276 ) ) ;
#21983=AXIS2_PLACEMENT_3D ( 'NONE', #96987, #31082, #75998 ) ;
#21984=ORIENTED_EDGE ( 'NONE', *, *, #83069, .F. ) ;
#21985=LINE ( 'NONE', #11808, #82444 ) ;
#21991=EDGE_LOOP ( 'NONE', ( #141786, #92607, #36848, #80062 ) ) ;
#21992=ORIENTED_EDGE ( 'NONE', *, *, #41328, .F. ) ;
#21993=CARTESIAN_POINT ( 'NONE',  ( 11.47599861414542843, 22.03583458319438648, 4.979811245910084949 ) ) ;
#21995=VECTOR ( 'NONE', #115145, 1000.000000000000000 ) ;
#21996=LINE ( 'NONE', #109731, #79187 ) ;
#21998=DIRECTION ( 'NONE',  ( -0.7071067811865487940, 0.7071067811865463515, 0.000000000000000000 ) ) ;
#21999=DIRECTION ( 'NONE',  ( 0.000000000000000000, 0.000000000000000000, 1.000000000000000000 ) ) ;
#22000=FACE_OUTER_BOUND ( 'NONE', #118143, .T. ) ;
#22002=ADVANCED_FACE ( 'NONE', ( #50308 ), #138748, .F. ) ;
#22003=FACE_BOUND ( 'NONE', #47709, .T. ) ;
#22004=CARTESIAN_POINT ( 'NONE',  ( -24.48921356237309510, -27.52281430457072631, 5.000000000000000000 ) ) ;
#22006=EDGE_CURVE ( 'NONE', #25093, #99900, #117653, .T. ) ;
#22007=DIRECTION ( 'NONE',  ( 0.6830127018922180770, -0.6830127018922204085, -0.2588190451025213501 ) ) ;
#22008=LINE ( 'NONE', #231, #20330 ) ;
#22009=VERTEX_POINT ( 'NONE', #28560 ) ;
#22013=VERTEX_POINT ( 'NONE', #18339 ) ;
#22014=VECTOR ( 'NONE', #97467, 1000.000000000000227 ) ;
#22015=ORIENTED_EDGE ( 'NONE', *, *, #97317, .T. ) ;
#22017=ORIENTED_EDGE ( 'NONE', *, *, #88915, .F. ) ;
#22018=CARTESIAN_POINT ( 'NONE',  ( -24.18398860626899705, 28.73617430169804265, 5.000000000000000000 ) ) ;
#22019=VECTOR ( 'NONE', #37590, 1000.000000000000000 ) ;
#22020=EDGE_CURVE ( 'NONE', #9775, #90465, #51743, .T. ) ;
#22021=PLANE ( 'NONE',  #95267 ) ;
#22022=VERTEX_POINT ( 'NONE', #43703 ) ;
#22023=LINE ( 'NONE', #90889, #90774 ) ;
#22024=ADVANCED_FACE ( 'NONE', ( #87209 ), #121950, .T. ) ;
#22025=CARTESIAN_POINT ( 'NONE',  ( 32.99999999999976552, 14.87792677143811026, -11.06722581663432337 ) ) ;
#22026=LINE ( 'NONE', #4309, #43731 ) ;
#22027=DIRECTION ( 'NONE',  ( -0.7071067811865486830, -0.7071067811865464625, 0.000000000000000000 ) ) ;
#22028=DIRECTION ( 'NONE',  ( -0.000000000000000000, -0.3543493200069152693, 0.9351131265310292928 ) ) ;
#22029=CARTESIAN_POINT ( 'NONE',  ( -1.499999999999980460, 8.319652575858389909, -8.582050562765831003 ) ) ;
#22030=DIRECTION ( 'NONE',  ( 1.000000000000000000, 0.000000000000000000, 0.000000000000000000 ) ) ;
#22031=DIRECTION ( 'NONE',  ( -0.6830127018922180770, -0.6830127018922204085, -0.2588190451025213501 ) ) ;
#22032=EDGE_LOOP ( 'NONE', ( #133697, #54661, #37369, #100716 ) ) ;
#22033=ADVANCED_FACE ( 'NONE', ( #100930 ), #77077, .F. ) ;
#22034=EDGE_LOOP ( 'NONE', ( #16635, #67585, #8510, #127008 ) ) ;
#22035=CARTESIAN_POINT ( 'NONE',  ( 4.499999999999968914, -7.533600742197662292, 5.000000000000000000 ) ) ;
#22036=ORIENTED_EDGE ( 'NONE', *, *, #82722, .T. ) ;
#22038=FACE_OUTER_BOUND ( 'NONE', #120546, .T. ) ;
#22039=VERTEX_POINT ( 'NONE', #122678 ) ;
#22041=LINE ( 'NONE', #43116, #51607 ) ;
#22043=DIRECTION ( 'NONE',  ( 0.7071067811865487940, 0.7071067811865463515, 0.000000000000000000 ) ) ;
#22044=VERTEX_POINT ( 'NONE', #67635 ) ;
#22045=CARTESIAN_POINT ( 'NONE',  ( 12.70710678118646619, -3.740707523384243505, 5.000000000000000000 ) ) ;
#22046=ADVANCED_FACE ( 'NONE', ( #11760 ), #45871, .F. ) ;
#22047=EDGE_LOOP ( 'NONE', ( #39713, #52697, #116089, #79360, #93251 ) ) ;
#22048=DIRECTION ( 'NONE',  ( 0.000000000000000000, 0.000000000000000000, 1.000000000000000000 ) ) ;
#22049=CARTESIAN_POINT ( 'NONE',  ( -62.99451991528749772, 28.92564299267982264, 4.000000000000000000 ) ) ;
#22050=VERTEX_POINT ( 'NONE', #20493 ) ;
#22051=VERTEX_POINT ( 'NONE', #88655 ) ;
#22052=DIRECTION ( 'NONE',  ( -0.000000000000000000, 0.3543493200069153248, 0.9351131265310292928 ) ) ;
#22054=ADVANCED_FACE ( 'NONE', ( #9617 ), #143014, .F. ) ;
#22055=EDGE_CURVE ( 'NONE', #35909, #108000, #23363, .T. ) ;
#22056=FACE_OUTER_BOUND ( 'NONE', #56220, .T. ) ;
#22057=VERTEX_POINT ( 'NONE', #21940 ) ;
#22058=DIRECTION ( 'NONE',  ( -0.7071067811865486830, -0.7071067811865464625, 0.000000000000000000 ) ) ;
#22059=ORIENTED_EDGE ( 'NONE', *, *, #60870, .F. ) ;
#22060=DIRECTION ( 'NONE',  ( -0.6830127018922181881, 0.6830127018922202975, -0.2588190451025214056 ) ) ;
#22061=CARTESIAN_POINT ( 'NONE',  ( 33.32816939922329880, -18.74070752338408852, 4.000000000000000000 ) ) ;
#22062=DIRECTION ( 'NONE',  ( 0.6830127018922181881, 0.6830127018922202975, -0.2588190451025214056 ) ) ;
#22063=EDGE_CURVE ( 'NONE', #30172, #93902, #133579, .T. ) ;
#22065=( BOUNDED_CURVE ( )  B_SPLINE_CURVE ( 3, ( #68892, #59451, #124672, #100782 ),
 .UNSPECIFIED., .F., .F. ) 
 B_SPLINE_CURVE_WITH_KNOTS ( ( 4, 4 ),
 ( 3.794322559382541371, 3.828945978481788526 ),
 .UNSPECIFIED. ) 
 CURVE ( )  GEOMETRIC_REPRESENTATION_ITEM ( )  RATIONAL_B_SPLINE_CURVE ( ( 1.000000000000000000, 0.9999001040657221617, 0.9999001040657221617, 1.000000000000000000 ) ) 
 REPRESENTATION_ITEM ( '' )  );
#22066=CARTESIAN_POINT ( 'NONE',  ( 23.99999999999983302, -13.06887692260768041, 4.000000000000000000 ) ) ;
#22067=DIRECTION ( 'NONE',  ( 0.6830127018922180770, -0.6830127018922204085, -0.2588190451025213501 ) ) ;
#22068=ADVANCED_FACE ( 'NONE', ( #90046 ), #32113, .F. ) ;
#22069=LINE ( 'NONE', #75770, #41406 ) ;
#22070=VERTEX_POINT ( 'NONE', #98090 ) ;
#22072=CARTESIAN_POINT ( 'NONE',  ( 36.48921356237310221, -27.52281430457080802, 5.000000000000000000 ) ) ;
#22074=CARTESIAN_POINT ( 'NONE',  ( 72.29974487139158157, -27.71228299555256669, 4.000000000000000000 ) ) ;
#22076=VECTOR ( 'NONE', #114157, 1000.000000000000000 ) ;
#22078=VERTEX_POINT ( 'NONE', #87917 ) ;
#22079=CARTESIAN_POINT ( 'NONE',  ( 23.20710678118638626, 9.759292476615614831, 5.000000000000000000 ) ) ;
#22080=CARTESIAN_POINT ( 'NONE',  ( 8.207106781186492839, 18.75929247661552779, 5.000000000000000000 ) ) ;
#22081=EDGE_CURVE ( 'NONE', #133528, #104648, #56770, .T. ) ;
#22082=LINE ( 'NONE', #99643, #62988 ) ;
#22084=ORIENTED_EDGE ( 'NONE', *, *, #132924, .F. ) ;
#22086=CARTESIAN_POINT ( 'NONE',  ( 13.49999999999990763, -4.216083040037239549, -7.486842126848689105 ) ) ;
#22087=LINE ( 'NONE', #57615, #60859 ) ;
#22089=EDGE_CURVE ( 'NONE', #134528, #105677, #34260, .T. ) ;
#22090=CARTESIAN_POINT ( 'NONE',  ( 33.29974487139158867, -27.71228299555229313, 4.000000000000000000 ) ) ;
#22092=DIRECTION ( 'NONE',  ( 0.6830127018922181881, 0.6830127018922202975, -0.2588190451025214056 ) ) ;
#22093=CARTESIAN_POINT ( 'NONE',  ( -30.70710678118633297, 14.25929247661557042, 5.000000000000000000 ) ) ;
#22094=AXIS2_PLACEMENT_3D ( 'NONE', #69391, #25866, #93265 ) ;
#22095=CARTESIAN_POINT ( 'NONE',  ( -51.18398860626899705, 28.73617430169823095, 5.000000000000000000 ) ) ;
#22096=ORIENTED_EDGE ( 'NONE', *, *, #10443, .F. ) ;
#22097=CARTESIAN_POINT ( 'NONE',  ( -57.18398860626899705, 28.73617430169827358, 5.000000000000000000 ) ) ;
#22098=ORIENTED_EDGE ( 'NONE', *, *, #78909, .F. ) ;
#22099=DIRECTION ( 'NONE',  ( -0.000000000000000000, -0.3543493200069152693, 0.9351131265310292928 ) ) ;
#22100=FACE_OUTER_BOUND ( 'NONE', #71314, .T. ) ;
#22102=CARTESIAN_POINT ( 'NONE',  ( -5.999999999999970690, 17.58746187583908238, 4.000000000000000000 ) ) ;
#22103=CARTESIAN_POINT ( 'NONE',  ( -20.99999999999985079, -15.03360074219758502, 5.000000000000000000 ) ) ;
#22104=DIRECTION ( 'NONE',  ( -0.000000000000000000, 0.3543493200069153248, 0.9351131265310292928 ) ) ;
#22105=CARTESIAN_POINT ( 'NONE',  ( -21.79289321881330466, -2.240707523384257716, 5.000000000000000000 ) ) ;
#22106=ORIENTED_EDGE ( 'NONE', *, *, #68604, .F. ) ;
#22107=VERTEX_POINT ( 'NONE', #132161 ) ;
#22108=DIRECTION ( 'NONE',  ( -0.7071067811865486830, -0.7071067811865464625, -0.000000000000000000 ) ) ;
#22109=EDGE_CURVE ( 'NONE', #108363, #53838, #120505, .T. ) ;
#22111=VECTOR ( 'NONE', #101483, 1000.000000000000000 ) ;
#22112=CARTESIAN_POINT ( 'NONE',  ( 26.99451991528749417, 28.92564299267956685, 4.000000000000000000 ) ) ;
#22115=CARTESIAN_POINT ( 'NONE',  ( -48.18398860626899705, 28.73617430169820608, 5.000000000000000000 ) ) ;
#22116=EDGE_CURVE ( 'NONE', #40495, #45983, #55308, .T. ) ;
#22117=PLANE ( 'NONE',  #117715 ) ;
#22118=ORIENTED_EDGE ( 'NONE', *, *, #75621, .T. ) ;
#22120=VECTOR ( 'NONE', #12431, 1000.000000000000000 ) ;
#22121=DIRECTION ( 'NONE',  ( 0.7071067811865487940, 0.7071067811865463515, 0.000000000000000000 ) ) ;
#22122=DIRECTION ( 'NONE',  ( 0.6830127018922180770, -0.6830127018922204085, -0.2588190451025213501 ) ) ;
#22123=DIRECTION ( 'NONE',  ( -0.7071067811865486830, -0.7071067811865464625, 0.000000000000000000 ) ) ;
#22125=ORIENTED_EDGE ( 'NONE', *, *, #117938, .F. ) ;
#22127=VERTEX_POINT ( 'NONE', #22622 ) ;
#22128=CARTESIAN_POINT ( 'NONE',  ( 15.18398860626900237, 28.73617430169797871, 5.000000000000000000 ) ) ;
#22130=CARTESIAN_POINT ( 'NONE',  ( 39.18398860626899705, 28.73617430169814568, 5.000000000000000000 ) ) ;
#22131=ORIENTED_EDGE ( 'NONE', *, *, #15863, .F. ) ;
#22132=CARTESIAN_POINT ( 'NONE',  ( -5.292986735706916690, -21.74070752338406010, 4.999753212805220670 ) ) ;
#22133=DIRECTION ( 'NONE',  ( 0.7071067811865487940, 0.7071067811865463515, 0.000000000000000000 ) ) ;
#22134=CARTESIAN_POINT ( 'NONE',  ( 7.499999999999951150, -5.947814304570770538, 5.000000000000000000 ) ) ;
#22136=DIRECTION ( 'NONE',  ( 0.6830127018922180770, -0.6830127018922204085, -0.2588190451025213501 ) ) ;
#22137=PLANE ( 'NONE',  #26747 ) ;
#22138=ORIENTED_EDGE ( 'NONE', *, *, #84518, .T. ) ;
#22139=PLANE ( 'NONE',  #27607 ) ;
#22140=DIRECTION ( 'NONE',  ( -0.000000000000000000, 0.000000000000000000, 1.000000000000000000 ) ) ;
#22142=CARTESIAN_POINT ( 'NONE',  ( 19.05000000000000071, 3.174999999999997158, 5.000000000000000000 ) ) ;
#22143=ORIENTED_EDGE ( 'NONE', *, *, #14981, .T. ) ;
#22144=ORIENTED_EDGE ( 'NONE', *, *, #20804, .F. ) ;
#22148=CARTESIAN_POINT ( 'NONE',  ( -14.51078643762690490, -27.52281430457045275, 5.000000000000000000 ) ) ;
#22149=DIRECTION ( 'NONE',  ( 0.6830127018922181881, 0.6830127018922202975, -0.2588190451025214056 ) ) ;
#22150=ADVANCED_FACE ( 'NONE', ( #92915 ), #38544, .T. ) ;
#22151=CARTESIAN_POINT ( 'NONE',  ( 0.000000000000000000, 0.000000000000000000, 5.000000000000000000 ) ) ;
#22153=ORIENTED_EDGE ( 'NONE', *, *, #82299, .F. ) ;
#22155=LINE ( 'NONE', #66415, #100086 ) ;
#22156=CARTESIAN_POINT ( 'NONE',  ( -11.70025512860841133, -27.71228299555198049, 4.000000000000000000 ) ) ;
#22157=ORIENTED_EDGE ( 'NONE', *, *, #40578, .T. ) ;
#22158=CARTESIAN_POINT ( 'NONE',  ( -18.10180811604841011, 9.068207373850700748, 5.000000000000000000 ) ) ;
#22159=PLANE ( 'NONE',  #34142 ) ;
#22160=CARTESIAN_POINT ( 'NONE',  ( -15.32816939922342492, -6.740707523384209310, 4.000000000000000000 ) ) ;
#22161=ORIENTED_EDGE ( 'NONE', *, *, #9603, .F. ) ;
#22162=EDGE_CURVE ( 'NONE', #42348, #89916, #60320, .T. ) ;
#22163=ADVANCED_FACE ( 'NONE', ( #24796 ), #93641, .F. ) ;
#22164=FACE_BOUND ( 'NONE', #53001, .T. ) ;
#22165=LINE ( 'NONE', #107051, #59380 ) ;
#22166=LINE ( 'NONE', #130974, #127655 ) ;
#22167=CARTESIAN_POINT ( 'NONE',  ( 24.48921356237309510, -27.52281430457072631, 5.000000000000000000 ) ) ;
#22169=EDGE_CURVE ( 'NONE', #48106, #66483, #4405, .T. ) ;
#22170=DIRECTION ( 'NONE',  ( 0.6830127018922180770, -0.6830127018922204085, -0.2588190451025213501 ) ) ;
#22172=VECTOR ( 'NONE', #114946, 1000.000000000000000 ) ;
#22174=ORIENTED_EDGE ( 'NONE', *, *, #10418, .T. ) ;
#22176=( BOUNDED_CURVE ( )  B_SPLINE_CURVE ( 3, ( #19053, #75590, #19761, #128541 ),
 .UNSPECIFIED., .F., .T. ) 
 B_SPLINE_CURVE_WITH_KNOTS ( ( 4, 4 ),
 ( 2.001653308786153218, 3.503810798801451742 ),
 .UNSPECIFIED. ) 
 CURVE ( )  GEOMETRIC_REPRESENTATION_ITEM ( )  RATIONAL_B_SPLINE_CURVE ( ( 1.000000000000000000, 0.8206354192515201706, 0.8206354192515201706, 1.000000000000000000 ) ) 
 REPRESENTATION_ITEM ( '' )  );
#22177=ORIENTED_EDGE ( 'NONE', *, *, #52232, .T. ) ;
#22179=EDGE_CURVE ( 'NONE', #25257, #391, #113225, .T. ) ;
#22180=ORIENTED_EDGE ( 'NONE', *, *, #7979, .T. ) ;
#22181=CARTESIAN_POINT ( 'NONE',  ( -36.18398860626899705, 28.73617430169812437, 5.000000000000000000 ) ) ;
#22182=DIRECTION ( 'NONE',  ( -0.7071067811865486830, -0.7071067811865464625, 0.000000000000000000 ) ) ;
#22183=ADVANCED_FACE ( 'NONE', ( #137870 ), #69046, .F. ) ;
#22185=VERTEX_POINT ( 'NONE', #81358 ) ;
#22186=LINE ( 'NONE', #25048, #120162 ) ;
#22187=FACE_OUTER_BOUND ( 'NONE', #139916, .T. ) ;
#22188=LINE ( 'NONE', #84790, #57000 ) ;
#22189=VECTOR ( 'NONE', #28257, 1000.000000000000227 ) ;
#22190=CARTESIAN_POINT ( 'NONE',  ( 8.999999999999937828, 2.342191155542461267, -5.001666872980106149 ) ) ;
#22192=CARTESIAN_POINT ( 'NONE',  ( -6.758600742197917732, 21.72500000000000142, 5.000000000000000000 ) ) ;
#22193=EDGE_CURVE ( 'NONE', #2860, #925, #48709, .T. ) ;
#22195=ORIENTED_EDGE ( 'NONE', *, *, #48238, .F. ) ;
#22196=CARTESIAN_POINT ( 'NONE',  ( -1.499999999999987566, -5.568876922607757685, 4.000000000000000000 ) ) ;
#22197=DIRECTION ( 'NONE',  ( -0.3543493200069162685, -0.000000000000000000, -0.9351131265310288487 ) ) ;
#22198=ORIENTED_EDGE ( 'NONE', *, *, #8714, .T. ) ;
#22199=ORIENTED_EDGE ( 'NONE', *, *, #15823, .T. ) ;
#22200=ORIENTED_EDGE ( 'NONE', *, *, #21378, .F. ) ;
#22202=EDGE_CURVE ( 'NONE', #82994, #125640, #15321, .T. ) ;
#22203=VERTEX_POINT ( 'NONE', #80631 ) ;
#22204=VECTOR ( 'NONE', #112213, 1000.000000000000000 ) ;
#22205=CARTESIAN_POINT ( 'NONE',  ( 54.18398860626899705, 28.73617430169825226, 5.000000000000000000 ) ) ;
#22206=AXIS2_PLACEMENT_3D ( 'NONE', #6065, #27140, #16231 ) ;
#22209=LINE ( 'NONE', #43288, #68070 ) ;
#22211=EDGE_CURVE ( 'NONE', #119191, #76747, #68355, .T. ) ;
#22212=VERTEX_POINT ( 'NONE', #135035 ) ;
#22214=VECTOR ( 'NONE', #82069, 1000.000000000000227 ) ;
#22215=LINE ( 'NONE', #20800, #19325 ) ;
#22216=CARTESIAN_POINT ( 'NONE',  ( -30.42356297102625717, -22.22500000000000142, 3.294237237169319599 ) ) ;
#22217=ADVANCED_FACE ( 'NONE', ( #92183 ), #71189, .F. ) ;
#22218=ORIENTED_EDGE ( 'NONE', *, *, #3710, .F. ) ;
#22219=DIRECTION ( 'NONE',  ( -0.7071067811865487940, 0.7071067811865463515, -0.000000000000000000 ) ) ;
#22220=ORIENTED_EDGE ( 'NONE', *, *, #70681, .F. ) ;
#22222=VERTEX_POINT ( 'NONE', #101643 ) ;
#22223=VERTEX_POINT ( 'NONE', #2300 ) ;
#22225=EDGE_CURVE ( 'NONE', #19559, #133451, #103087, .T. ) ;
#22227=CARTESIAN_POINT ( 'NONE',  ( 8.510786437626906675, -27.52281430457049183, 5.000000000000000000 ) ) ;
#22229=DIRECTION ( 'NONE',  ( -0.3543493200069162685, -0.000000000000000000, -0.9351131265310288487 ) ) ;
#22230=ORIENTED_EDGE ( 'NONE', *, *, #108130, .F. ) ;
#22232=CARTESIAN_POINT ( 'NONE',  ( -28.49999999999979750, 0.4497235411627178991, -5.599840258123606418 ) ) ;
#22234=ADVANCED_FACE ( 'NONE', ( #90799 ), #3040, .F. ) ;
#22235=LINE ( 'NONE', #23690, #123105 ) ;
#22236=ORIENTED_EDGE ( 'NONE', *, *, #62733, .T. ) ;
#22237=VERTEX_POINT ( 'NONE', #14647 ) ;
#22238=ORIENTED_EDGE ( 'NONE', *, *, #117375, .F. ) ;
#22239=FACE_OUTER_BOUND ( 'NONE', #101063, .T. ) ;
#22240=AXIS2_PLACEMENT_3D ( 'NONE', #136785, #37496, #81732 ) ;
#22241=DIRECTION ( 'NONE',  ( -0.000000000000000000, 0.3543493200069153248, 0.9351131265310292928 ) ) ;
#22243=LINE ( 'NONE', #67969, #80705 ) ;
#22244=CARTESIAN_POINT ( 'NONE',  ( -14.11732500641695509, -0.1862019290248694003, 4.000000000000000000 ) ) ;
#22246=LINE ( 'NONE', #56385, #67209 ) ;
#22248=EDGE_LOOP ( 'NONE', ( #12815, #2961, #143267 ) ) ;
#22249=DIRECTION ( 'NONE',  ( -0.000000000000000000, 0.000000000000000000, 1.000000000000000000 ) ) ;
#22250=VECTOR ( 'NONE', #46785, 1000.000000000000227 ) ;
#22251=ORIENTED_EDGE ( 'NONE', *, *, #44468, .F. ) ;
#22252=PLANE ( 'NONE',  #75446 ) ;
#22253=ORIENTED_EDGE ( 'NONE', *, *, #26505, .F. ) ;
#22255=PLANE ( 'NONE',  #76557 ) ;
#22256=EDGE_LOOP ( 'NONE', ( #127565, #13290, #8907, #120617 ) ) ;
#22257=LINE ( 'NONE', #110001, #141835 ) ;
#22258=ORIENTED_EDGE ( 'NONE', *, *, #88510, .T. ) ;
#22260=LINE ( 'NONE', #66526, #102317 ) ;
#22262=AXIS2_PLACEMENT_3D ( 'NONE', #99573, #112619, #80036 ) ;
#22263=ADVANCED_FACE ( 'NONE', ( #7310 ), #63879, .F. ) ;
#22266=VECTOR ( 'NONE', #65746, 1000.000000000000000 ) ;
#22268=DIRECTION ( 'NONE',  ( -0.000000000000000000, 0.000000000000000000, -1.000000000000000000 ) ) ;
#22269=CARTESIAN_POINT ( 'NONE',  ( -32.47599861414528277, 22.03583458319437938, 4.979811245910089390 ) ) ;
#22272=CARTESIAN_POINT ( 'NONE',  ( 66.48921356237309510, -27.52281430457101763, 5.000000000000000000 ) ) ;
#22273=CARTESIAN_POINT ( 'NONE',  ( -6.299744871391586898, -27.71228299555210484, 4.000000000000000000 ) ) ;
#22274=ORIENTED_EDGE ( 'NONE', *, *, #134730, .T. ) ;
#22275=ORIENTED_EDGE ( 'NONE', *, *, #89769, .F. ) ;
#22276=CARTESIAN_POINT ( 'NONE',  ( 26.20710678118636494, 18.75929247661552068, 5.000000000000000000 ) ) ;
#22277=EDGE_LOOP ( 'NONE', ( #133100, #98973, #102516, #65036 ) ) ;
#22278=VECTOR ( 'NONE', #10588, 999.9999999999998863 ) ;
#22280=LINE ( 'NONE', #113597, #124984 ) ;
#22282=DIRECTION ( 'NONE',  ( 0.3543493200069163240, -0.000000000000000000, -0.9351131265310288487 ) ) ;
#22283=EDGE_LOOP ( 'NONE', ( #99470, #44289, #67365, #37546 ) ) ;
#22284=CARTESIAN_POINT ( 'NONE',  ( -30.48921356237309510, -27.52281430457076894, 5.000000000000000000 ) ) ;
#22286=VECTOR ( 'NONE', #51964, 1000.000000000000000 ) ;
#22288=LINE ( 'NONE', #78151, #30962 ) ;
#22289=CARTESIAN_POINT ( 'NONE',  ( -31.82334089840007607, 5.259292476615665457, 15.86257073897105130 ) ) ;
#22290=VERTEX_POINT ( 'NONE', #82767 ) ;
#22292=CARTESIAN_POINT ( 'NONE',  ( -33.79289321881321939, -8.240707523384195099, 5.000000000000000000 ) ) ;
#22295=AXIS2_PLACEMENT_3D ( 'NONE', #68393, #21980, #87964 ) ;
#22296=CARTESIAN_POINT ( 'NONE',  ( 25.49999999999982236, 21.05218569542895324, 5.000000000000000000 ) ) ;
#22297=VECTOR ( 'NONE', #141653, 1000.000000000000000 ) ;
#22298=ORIENTED_EDGE ( 'NONE', *, *, #138071, .T. ) ;
#22299=ORIENTED_EDGE ( 'NONE', *, *, #72244, .T. ) ;
#22300=VERTEX_POINT ( 'NONE', #129105 ) ;
#22301=VECTOR ( 'NONE', #4028, 1000.000000000000227 ) ;
#22303=ORIENTED_EDGE ( 'NONE', *, *, #241, .T. ) ;
#22304=FACE_OUTER_BOUND ( 'NONE', #64503, .T. ) ;
#22306=DIRECTION ( 'NONE',  ( 0.7071067811865487940, 0.7071067811865463515, 0.000000000000000000 ) ) ;
#22307=AXIS2_PLACEMENT_3D ( 'NONE', #14461, #136229, #36916 ) ;
#22308=CARTESIAN_POINT ( 'NONE',  ( 20.99999999999985079, -18.41253812416056590, 4.000000000000000000 ) ) ;
#22309=ORIENTED_EDGE ( 'NONE', *, *, #23651, .T. ) ;
#22310=FACE_OUTER_BOUND ( 'NONE', #99579, .T. ) ;
#22311=CARTESIAN_POINT ( 'NONE',  ( 28.49999999999980460, 21.43112307739196254, 4.000000000000000000 ) ) ;
#22313=ORIENTED_EDGE ( 'NONE', *, *, #83440, .T. ) ;
#22314=CARTESIAN_POINT ( 'NONE',  ( -26.14994871458959480, -8.240707523384193323, 17.25253755692233071 ) ) ;
#22315=EDGE_CURVE ( 'NONE', #86742, #116142, #117495, .T. ) ;
#22316=LINE ( 'NONE', #11441, #116437 ) ;
#22317=EDGE_LOOP ( 'NONE', ( #69648, #134974, #78260, #54533, #37720 ) ) ;
#22318=ORIENTED_EDGE ( 'NONE', *, *, #50395, .F. ) ;
#22319=ORIENTED_EDGE ( 'NONE', *, *, #54477, .F. ) ;
#22320=CARTESIAN_POINT ( 'NONE',  ( 27.48921356237309155, -27.52281430457074762, 5.000000000000000000 ) ) ;
#22321=EDGE_CURVE ( 'NONE', #91520, #50934, #85592, .T. ) ;
#22322=ADVANCED_FACE ( 'NONE', ( #17487 ), #108040, .F. ) ;
#22323=PLANE ( 'NONE',  #105481 ) ;
#22325=LINE ( 'NONE', #10051, #30366 ) ;
#22326=LINE ( 'NONE', #31118, #128997 ) ;
#22327=DIRECTION ( 'NONE',  ( -0.7071067811865486830, -0.7071067811865464625, -0.000000000000000000 ) ) ;
#22328=EDGE_CURVE ( 'NONE', #65622, #29125, #73327, .T. ) ;
#22329=EDGE_CURVE ( 'NONE', #22380, #13798, #40690, .T. ) ;
#22330=CARTESIAN_POINT ( 'NONE',  ( -21.48921356237309155, -27.52281430457070499, 5.000000000000000000 ) ) ;
#22331=AXIS2_PLACEMENT_3D ( 'NONE', #67016, #128180, #62208 ) ;
#22332=EDGE_CURVE ( 'NONE', #48528, #131664, #84894, .T. ) ;
#22333=VERTEX_POINT ( 'NONE', #128414 ) ;
#22334=ORIENTED_EDGE ( 'NONE', *, *, #49438, .F. ) ;
#22336=EDGE_CURVE ( 'NONE', #129163, #43341, #72646, .T. ) ;
#22337=VERTEX_POINT ( 'NONE', #118213 ) ;
#22339=VECTOR ( 'NONE', #85612, 1000.000000000000000 ) ;
#22340=ADVANCED_FACE ( 'NONE', ( #18919 ), #5873, .F. ) ;
#22341=EDGE_CURVE ( 'NONE', #42198, #962, #8706, .T. ) ;
#22342=CARTESIAN_POINT ( 'NONE',  ( 0.000000000000000000, 0.000000000000000000, 5.000000000000000000 ) ) ;
#22343=VERTEX_POINT ( 'NONE', #27647 ) ;
#22344=DIRECTION ( 'NONE',  ( 0.6830127018922180770, -0.6830127018922204085, -0.2588190451025213501 ) ) ;
#22345=PLANE ( 'NONE',  #81941 ) ;
#22346=DIRECTION ( 'NONE',  ( 0.7071067811865486830, -0.7071067811865464625, -0.000000000000000000 ) ) ;
#22347=VECTOR ( 'NONE', #41535, 1000.000000000000000 ) ;
#22348=DIRECTION ( 'NONE',  ( 1.000000000000000000, 0.000000000000000000, 0.000000000000000000 ) ) ;
#22349=CARTESIAN_POINT ( 'NONE',  ( -2.999999999999978240, 16.93112307739200872, 4.000000000000000000 ) ) ;
#22350=ORIENTED_EDGE ( 'NONE', *, *, #112077, .F. ) ;
#22351=EDGE_CURVE ( 'NONE', #139777, #10041, #52959, .T. ) ;
#22353=VECTOR ( 'NONE', #28981, 1000.000000000000000 ) ;
#22354=ORIENTED_EDGE ( 'NONE', *, *, #14990, .T. ) ;
#22355=CARTESIAN_POINT ( 'NONE',  ( -25.49999999999981881, 10.08746187583913922, 4.000000000000000000 ) ) ;
#22356=VERTEX_POINT ( 'NONE', #74765 ) ;
#22357=DIRECTION ( 'NONE',  ( 0.7071067811865487940, 0.7071067811865463515, 0.000000000000000000 ) ) ;
#22358=ORIENTED_EDGE ( 'NONE', *, *, #14618, .T. ) ;
#22359=DIRECTION ( 'NONE',  ( 0.6830127018922180770, -0.6830127018922202975, -0.2588190451025213501 ) ) ;
#22360=EDGE_LOOP ( 'NONE', ( #25490, #80496, #53408, #87337 ) ) ;
#22361=VERTEX_POINT ( 'NONE', #97156 ) ;
#22362=EDGE_CURVE ( 'NONE', #27746, #53886, #141422, .T. ) ;
#22363=ORIENTED_EDGE ( 'NONE', *, *, #91810, .T. ) ;
#22364=VECTOR ( 'NONE', #100154, 1000.000000000000000 ) ;
#22365=DIRECTION ( 'NONE',  ( 0.6830127018922180770, -0.6830127018922204085, -0.2588190451025213501 ) ) ;
#22366=DIRECTION ( 'NONE',  ( -0.7071067811865487940, 0.7071067811865463515, 0.000000000000000000 ) ) ;
#22368=DIRECTION ( 'NONE',  ( -0.7071067811865486830, 0.7071067811865464625, 0.000000000000000000 ) ) ;
#22369=AXIS2_PLACEMENT_3D ( 'NONE', #27173, #125801, #14874 ) ;
#22373=DIRECTION ( 'NONE',  ( 0.3543493200069162685, -0.000000000000000000, -0.9351131265310288487 ) ) ;
#22376=ADVANCED_FACE ( 'NONE', ( #61062 ), #105903, .F. ) ;
#22377=ORIENTED_EDGE ( 'NONE', *, *, #80164, .F. ) ;
#22378=CARTESIAN_POINT ( 'NONE',  ( -50.99451991528749062, 28.92564299267973738, 4.000000000000000000 ) ) ;
#22379=DIRECTION ( 'NONE',  ( 0.7071067811865487940, 0.7071067811865463515, 0.000000000000000000 ) ) ;
#22380=VERTEX_POINT ( 'NONE', #50140 ) ;
#22382=VERTEX_POINT ( 'NONE', #12323 ) ;
#22383=EDGE_LOOP ( 'NONE', ( #44938, #88409, #95510 ) ) ;
#22384=DIRECTION ( 'NONE',  ( -0.7071067811865486830, -0.7071067811865464625, 0.000000000000000000 ) ) ;
#22385=VERTEX_POINT ( 'NONE', #99315 ) ;
#22386=EDGE_CURVE ( 'NONE', #11167, #2296, #87044, .T. ) ;
#22387=ORIENTED_EDGE ( 'NONE', *, *, #30216, .T. ) ;
#22388=CARTESIAN_POINT ( 'NONE',  ( -11.99451991528749417, 28.92564299267946382, 4.000000000000000000 ) ) ;
#22391=LINE ( 'NONE', #118331, #33391 ) ;
#22392=DIRECTION ( 'NONE',  ( 0.3543493200069162685, -0.000000000000000000, -0.9351131265310288487 ) ) ;
#22393=EDGE_LOOP ( 'NONE', ( #68227, #68323, #22953, #139223 ) ) ;
#22394=DIRECTION ( 'NONE',  ( -0.7071067811865486830, 0.7071067811865464625, 0.000000000000000000 ) ) ;
#22396=VECTOR ( 'NONE', #87085, 1000.000000000000000 ) ;
#22397=VECTOR ( 'NONE', #107406, 1000.000000000000000 ) ;
#22400=VECTOR ( 'NONE', #52783, 1000.000000000000000 ) ;
#22402=ORIENTED_EDGE ( 'NONE', *, *, #2885, .F. ) ;
#22404=DIRECTION ( 'NONE',  ( -0.7071067811865486830, -0.7071067811865464625, 0.000000000000000000 ) ) ;
#22405=EDGE_CURVE ( 'NONE', #124775, #80852, #719, .T. ) ;
#22406=CARTESIAN_POINT ( 'NONE',  ( 27.48921356237309155, -27.52281430457074762, 5.000000000000000000 ) ) ;
#22407=EDGE_LOOP ( 'NONE', ( #46622, #11570, #9179, #3624, #109864, #137690 ) ) ;
#22408=VECTOR ( 'NONE', #54982, 1000.000000000000000 ) ;
#22409=ORIENTED_EDGE ( 'NONE', *, *, #44892, .F. ) ;
#22410=EDGE_LOOP ( 'NONE', ( #83547, #50713, #97423, #21574 ) ) ;
#22411=DIRECTION ( 'NONE',  ( 0.6830127018922181881, 0.6830127018922202975, -0.2588190451025214056 ) ) ;
#22412=LINE ( 'NONE', #12972, #12 ) ;
#22413=DIRECTION ( 'NONE',  ( 0.3543493200069162685, -0.000000000000000000, -0.9351131265310288487 ) ) ;
#22414=AXIS2_PLACEMENT_3D ( 'NONE', #128448, #29119, #116117 ) ;
#22420=ADVANCED_FACE ( 'NONE', ( #109505 ), #116564, .F. ) ;
#22421=DIRECTION ( 'NONE',  ( 0.7071067811865486830, -0.7071067811865464625, -0.000000000000000000 ) ) ;
#22422=DIRECTION ( 'NONE',  ( 0.6830127018922180770, -0.6830127018922204085, -0.2588190451025213501 ) ) ;
#22423=VERTEX_POINT ( 'NONE', #64573 ) ;
#22424=CARTESIAN_POINT ( 'NONE',  ( -34.49999999999975842, 22.21934299833216997, 4.348028800457638177 ) ) ;
#22425=CARTESIAN_POINT ( 'NONE',  ( -23.99451991528749062, 28.92564299267954908, 4.000000000000000000 ) ) ;
#22426=ORIENTED_EDGE ( 'NONE', *, *, #121619, .T. ) ;
#22427=LINE ( 'NONE', #119599, #27788 ) ;
#22428=VERTEX_POINT ( 'NONE', #9439 ) ;
#22429=EDGE_CURVE ( 'NONE', #121175, #22931, #100069, .T. ) ;
#22430=VERTEX_POINT ( 'NONE', #53720 ) ;
#22431=PLANE ( 'NONE',  #67923 ) ;
#22432=PLANE ( 'NONE',  #136362 ) ;
#22433=VECTOR ( 'NONE', #44384, 1000.000000000000000 ) ;
#22434=VERTEX_POINT ( 'NONE', #31947 ) ;
#22435=LINE ( 'NONE', #111623, #79057 ) ;
#22437=CIRCLE ( 'NONE', #8554, 5.968999999999998529 ) ;
#22438=DIRECTION ( 'NONE',  ( 0.3543493200069162685, -0.000000000000000000, -0.9351131265310288487 ) ) ;
#22439=PLANE ( 'NONE',  #4474 ) ;
#22441=CARTESIAN_POINT ( 'NONE',  ( -6.328169399223481761, -6.740707523384218192, 4.000000000000000000 ) ) ;
#22442=CARTESIAN_POINT ( 'NONE',  ( 3.668467411598555383, -18.74070752338408496, 20.73178291233841719 ) ) ;
#22443=CARTESIAN_POINT ( 'NONE',  ( 31.49999999999977973, -14.56887692260766443, 4.000000000000000000 ) ) ;
#22444=DIRECTION ( 'NONE',  ( -0.6830127018922181881, 0.6830127018922202975, -0.2588190451025214056 ) ) ;
#22446=CARTESIAN_POINT ( 'NONE',  ( 32.99999999999977263, 7.007997736742474615, -8.085015511992036608 ) ) ;
#22449=FACE_OUTER_BOUND ( 'NONE', #86826, .T. ) ;
#22450=CARTESIAN_POINT ( 'NONE',  ( -6.005480084712508493, 28.92564299267933947, 4.000000000000000000 ) ) ;
#22451=ORIENTED_EDGE ( 'NONE', *, *, #21947, .F. ) ;
#22453=ADVANCED_FACE ( 'NONE', ( #67464 ), #78315, .F. ) ;
#22454=EDGE_LOOP ( 'NONE', ( #25449, #69268, #91917, #58359 ) ) ;
#22456=ADVANCED_FACE ( 'NONE', ( #142159 ), #88486, .F. ) ;
#22457=ORIENTED_EDGE ( 'NONE', *, *, #128123, .T. ) ;
#22458=ORIENTED_EDGE ( 'NONE', *, *, #75768, .T. ) ;
#22461=FACE_OUTER_BOUND ( 'NONE', #57239, .T. ) ;
#22462=DIRECTION ( 'NONE',  ( 1.000000000000000000, 0.000000000000000000, 0.000000000000000000 ) ) ;
#22463=VERTEX_POINT ( 'NONE', #111655 ) ;
#22464=CARTESIAN_POINT ( 'NONE',  ( -27.48921356237309155, -27.52281430457074762, 5.000000000000000000 ) ) ;
#22465=CARTESIAN_POINT ( 'NONE',  ( 8.816011393731004731, 28.73617430169781173, 5.000000000000000000 ) ) ;
#22466=CARTESIAN_POINT ( 'NONE',  ( -18.29974487139159223, -27.71228299555219010, 4.000000000000000000 ) ) ;
#22467=DIRECTION ( 'NONE',  ( 0.7071067811865487940, 0.7071067811865463515, 0.000000000000000000 ) ) ;
#22470=LINE ( 'NONE', #45018, #118243 ) ;
#22471=DIRECTION ( 'NONE',  ( -0.6830127018922180770, -0.6830127018922204085, -0.2588190451025213501 ) ) ;
#22472=CARTESIAN_POINT ( 'NONE',  ( -19.49999999999986144, -2.947814304570804289, 5.000000000000000000 ) ) ;
#22473=FACE_OUTER_BOUND ( 'NONE', #30191, .T. ) ;
#22474=DIRECTION ( 'NONE',  ( 0.7071067811865487940, -0.7071067811865463515, 0.000000000000000000 ) ) ;
#22475=CARTESIAN_POINT ( 'NONE',  ( -45.29974487139158867, -27.71228299555237840, 4.000000000000000000 ) ) ;
#22476=CARTESIAN_POINT ( 'NONE',  ( 22.60343192894629638, -14.24070752338413293, 19.24067776001730934 ) ) ;
#22477=ORIENTED_EDGE ( 'NONE', *, *, #68076, .F. ) ;
#22478=ORIENTED_EDGE ( 'NONE', *, *, #136792, .T. ) ;
#22480=VECTOR ( 'NONE', #102462, 999.9999999999998863 ) ;
#22481=ORIENTED_EDGE ( 'NONE', *, *, #32698, .T. ) ;
#22482=DIRECTION ( 'NONE',  ( -4.681814790819591790E-17, -0.3543493200069152693, 0.9351131265310292928 ) ) ;
#22484=DIRECTION ( 'NONE',  ( -0.7071067811865487940, 0.7071067811865463515, 0.000000000000000000 ) ) ;
#22485=CARTESIAN_POINT ( 'NONE',  ( -9.707013264292978505, -21.74070752338405654, 4.999753212805220670 ) ) ;
#22487=ORIENTED_EDGE ( 'NONE', *, *, #113509, .F. ) ;
#22489=DIRECTION ( 'NONE',  ( -0.000000000000000000, 0.000000000000000000, 1.000000000000000000 ) ) ;
#22490=CARTESIAN_POINT ( 'NONE',  ( 24.70710678118636494, 5.259292476615655687, 5.000000000000000000 ) ) ;
#22492=ORIENTED_EDGE ( 'NONE', *, *, #69820, .T. ) ;
#22495=ORIENTED_EDGE ( 'NONE', *, *, #131907, .T. ) ;
#22496=CARTESIAN_POINT ( 'NONE',  ( 25.49999999999982947, 12.05218569542904561, 5.000000000000000000 ) ) ;
#22497=EDGE_CURVE ( 'NONE', #47367, #32623, #77616, .T. ) ;
#22498=CARTESIAN_POINT ( 'NONE',  ( -34.47516574401892342, -8.971932658884083978, 4.998110765256835286 ) ) ;
#22499=LINE ( 'NONE', #109543, #43840 ) ;
#22500=AXIS2_PLACEMENT_3D ( 'NONE', #133119, #122188, #111319 ) ;
#22501=VECTOR ( 'NONE', #33297, 1000.000000000000000 ) ;
#22502=AXIS2_PLACEMENT_3D ( 'NONE', #36952, #91371, #26096 ) ;
#22503=EDGE_CURVE ( 'NONE', #89327, #62049, #131260, .T. ) ;
#22507=PLANE ( 'NONE',  #3862 ) ;
#22508=ADVANCED_FACE ( 'NONE', ( #26075 ), #36242, .F. ) ;
#22509=ORIENTED_EDGE ( 'NONE', *, *, #89192, .T. ) ;
#22510=ORIENTED_EDGE ( 'NONE', *, *, #114779, .F. ) ;
#22511=VECTOR ( 'NONE', #91208, 1000.000000000000000 ) ;
#22513=EDGE_CURVE ( 'NONE', #56805, #68414, #58754, .T. ) ;
#22514=FACE_OUTER_BOUND ( 'NONE', #116631, .T. ) ;
#22515=PLANE ( 'NONE',  #468 ) ;
#22516=ORIENTED_EDGE ( 'NONE', *, *, #136201, .T. ) ;
#22519=CARTESIAN_POINT ( 'NONE',  ( -30.18398860626900060, 28.73617430169808173, 5.000000000000000000 ) ) ;
#22521=CARTESIAN_POINT ( 'NONE',  ( 2.999999999999981792, 12.25461709320621218, -10.07315571508696550 ) ) ;
#22522=EDGE_CURVE ( 'NONE', #32821, #129523, #103599, .T. ) ;
#22523=FACE_BOUND ( 'NONE', #120254, .T. ) ;
#22525=EDGE_CURVE ( 'NONE', #71456, #71262, #125391, .T. ) ;
#22526=LINE ( 'NONE', #67525, #88443 ) ;
#22527=ORIENTED_EDGE ( 'NONE', *, *, #131088, .F. ) ;
#22529=ORIENTED_EDGE ( 'NONE', *, *, #99440, .T. ) ;
#22531=ORIENTED_EDGE ( 'NONE', *, *, #108806, .T. ) ;
#22532=DIRECTION ( 'NONE',  ( -0.000000000000000000, -0.3543493200069152693, 0.9351131265310292928 ) ) ;
#22533=EDGE_CURVE ( 'NONE', #63799, #38880, #4236, .T. ) ;
#22534=ORIENTED_EDGE ( 'NONE', *, *, #101467, .F. ) ;
#22536=VERTEX_POINT ( 'NONE', #123968 ) ;
#22537=LINE ( 'NONE', #100846, #99616 ) ;
#22539=DIRECTION ( 'NONE',  ( 0.7071067811865487940, -0.7071067811865463515, 0.000000000000000000 ) ) ;
#22540=EDGE_LOOP ( 'NONE', ( #85478, #104753, #35434, #15432 ) ) ;
#22541=DIRECTION ( 'NONE',  ( 0.7071067811865487940, 0.7071067811865463515, 0.000000000000000000 ) ) ;
#22543=AXIS2_PLACEMENT_3D ( 'NONE', #54128, #21465, #75162 ) ;
#22544=CARTESIAN_POINT ( 'NONE',  ( 20.99999999999985079, 4.384688058510579189, -7.090945410444635222 ) ) ;
#22545=CARTESIAN_POINT ( 'NONE',  ( 7.499999999999956479, 3.052185695429141976, 5.000000000000000000 ) ) ;
#22546=PLANE ( 'NONE',  #36596 ) ;
#22547=CARTESIAN_POINT ( 'NONE',  ( 29.29289321881325137, 2.259292476615696099, 5.000000000000000000 ) ) ;
#22548=CARTESIAN_POINT ( 'NONE',  ( -15.48921356237309510, -27.52281430457066236, 5.000000000000000000 ) ) ;
#22549=ORIENTED_EDGE ( 'NONE', *, *, #16848, .F. ) ;
#22550=ADVANCED_FACE ( 'NONE', ( #79787 ), #124662, .F. ) ;
#22551=ORIENTED_EDGE ( 'NONE', *, *, #37365, .T. ) ;
#22552=ORIENTED_EDGE ( 'NONE', *, *, #42010, .T. ) ;
#22553=CARTESIAN_POINT ( 'NONE',  ( -9.005480084712511157, 28.92564299267931816, 4.000000000000000000 ) ) ;
#22554=CARTESIAN_POINT ( 'NONE',  ( 30.48921356237309510, -27.52281430457076894, 5.000000000000000000 ) ) ;
#22555=ORIENTED_EDGE ( 'NONE', *, *, #42660, .T. ) ;
#22556=ORIENTED_EDGE ( 'NONE', *, *, #84416, .F. ) ;
#22557=CARTESIAN_POINT ( 'NONE',  ( 23.81601139373100295, 28.73617430169770870, 5.000000000000000000 ) ) ;
#22558=CARTESIAN_POINT ( 'NONE',  ( 60.18398860626900415, 28.73617430169829490, 5.000000000000000000 ) ) ;
#22559=VERTEX_POINT ( 'NONE', #114482 ) ;
#22560=PLANE ( 'NONE',  #129675 ) ;
#22561=ADVANCED_FACE ( 'NONE', ( #26772 ), #47859, .T. ) ;
#22564=FACE_OUTER_BOUND ( 'NONE', #24900, .T. ) ;
#22565=ORIENTED_EDGE ( 'NONE', *, *, #31891, .F. ) ;
#22568=LINE ( 'NONE', #87865, #88235 ) ;
#22569=EDGE_CURVE ( 'NONE', #45966, #82836, #2125, .T. ) ;
#22571=DIRECTION ( 'NONE',  ( 0.7071067811865486830, -0.7071067811865464625, -0.000000000000000000 ) ) ;
#22573=CARTESIAN_POINT ( 'NONE',  ( 42.18398860626899705, 28.73617430169816700, 5.000000000000000000 ) ) ;
#22574=ORIENTED_EDGE ( 'NONE', *, *, #105326, .T. ) ;
#22575=DIRECTION ( 'NONE',  ( -0.6830127018922180770, -0.6830127018922204085, -0.2588190451025213501 ) ) ;
#22577=DIRECTION ( 'NONE',  ( -0.6830127018922180770, -0.6830127018922204085, -0.2588190451025213501 ) ) ;
#22579=ORIENTED_EDGE ( 'NONE', *, *, #38590, .T. ) ;
#22580=CARTESIAN_POINT ( 'NONE',  ( 24.48921356237309510, -27.52281430457072631, 5.000000000000000000 ) ) ;
#22582=ADVANCED_FACE ( 'NONE', ( #81916 ), #90626, .F. ) ;
#22583=DIRECTION ( 'NONE',  ( 0.7071067811865486830, -0.7071067811865464625, -0.000000000000000000 ) ) ;
#22585=ORIENTED_EDGE ( 'NONE', *, *, #143458, .F. ) ;
#22586=DIRECTION ( 'NONE',  ( -0.000000000000000000, 0.3543493200069153248, 0.9351131265310292928 ) ) ;
#22589=ORIENTED_EDGE ( 'NONE', *, *, #59113, .F. ) ;
#22590=CARTESIAN_POINT ( 'NONE',  ( -68.99451991528748351, 28.92564299267986172, 4.000000000000000000 ) ) ;
#22592=ORIENTED_EDGE ( 'NONE', *, *, #71343, .F. ) ;
#22595=ORIENTED_EDGE ( 'NONE', *, *, #126752, .T. ) ;
#22596=FACE_OUTER_BOUND ( 'NONE', #70736, .T. ) ;
#22597=DIRECTION ( 'NONE',  ( 0.6830127018922180770, -0.6830127018922204085, -0.2588190451025213501 ) ) ;
#22598=AXIS2_PLACEMENT_3D ( 'NONE', #82491, #38976, #81074 ) ;
#22599=ORIENTED_EDGE ( 'NONE', *, *, #28561, .F. ) ;
#22600=AXIS2_PLACEMENT_3D ( 'NONE', #127777, #28463, #74098 ) ;
#22601=CARTESIAN_POINT ( 'NONE',  ( -34.92500000000001137, -22.22500000000000142, 4.000000000000000000 ) ) ;
#22602=LINE ( 'NONE', #99458, #123208 ) ;
#22604=PLANE ( 'NONE',  #125312 ) ;
#22605=CARTESIAN_POINT ( 'NONE',  ( 2.999999999999979128, -18.41253812416056945, 4.000000000000000000 ) ) ;
#22606=LINE ( 'NONE', #68339, #9990 ) ;
#22607=CARTESIAN_POINT ( 'NONE',  ( -5.999999999999970690, -16.02097659208072855, -11.96015758381207483 ) ) ;
#22610=EDGE_CURVE ( 'NONE', #121879, #65772, #49760, .T. ) ;
#22611=EDGE_LOOP ( 'NONE', ( #50215, #59343, #48469, #36546 ) ) ;
#22612=VERTEX_POINT ( 'NONE', #23937 ) ;
#22613=CARTESIAN_POINT ( 'NONE',  ( 2.700255128608413990, -27.71228299555204089, 4.000000000000000000 ) ) ;
#22615=ORIENTED_EDGE ( 'NONE', *, *, #130929, .F. ) ;
#22616=ORIENTED_EDGE ( 'NONE', *, *, #75264, .T. ) ;
#22617=CARTESIAN_POINT ( 'NONE',  ( -7.499999999999947597, -11.56887692260769818, 4.000000000000000000 ) ) ;
#22618=CARTESIAN_POINT ( 'NONE',  ( -8.475998614145453303, 22.03583458319437938, 4.979811245910092055 ) ) ;
#22619=VERTEX_POINT ( 'NONE', #13025 ) ;
#22621=FACE_OUTER_BOUND ( 'NONE', #86197, .T. ) ;
#22622=CARTESIAN_POINT ( 'NONE',  ( 10.82816939922345689, -5.240707523384232402, 4.000000000000000000 ) ) ;
#22623=LINE ( 'NONE', #133581, #7016 ) ;
#22625=VERTEX_POINT ( 'NONE', #13730 ) ;
#22626=EDGE_CURVE ( 'NONE', #42005, #96774, #102221, .T. ) ;
#22627=LINE ( 'NONE', #20497, #34879 ) ;
#22628=LINE ( 'NONE', #77082, #118636 ) ;
#22629=CIRCLE ( 'NONE', #17968, 5.968999999999998529 ) ;
#22630=LINE ( 'NONE', #99487, #58899 ) ;
#22633=( BOUNDED_CURVE ( )  B_SPLINE_CURVE ( 3, ( #20657, #141762, #119949, #40319 ),
 .UNSPECIFIED., .F., .T. ) 
 B_SPLINE_CURVE_WITH_KNOTS ( ( 4, 4 ),
 ( 1.864375635226939387, 1.933014472006533868 ),
 .UNSPECIFIED. ) 
 CURVE ( )  GEOMETRIC_REPRESENTATION_ITEM ( )  RATIONAL_B_SPLINE_CURVE ( ( 1.000000000000000000, 0.9996074310407766506, 0.9996074310407766506, 1.000000000000000000 ) ) 
 REPRESENTATION_ITEM ( '' )  );
#22634=DIRECTION ( 'NONE',  ( 0.6830127018922181881, 0.6830127018922202975, -0.2588190451025214056 ) ) ;
#22638=DIRECTION ( 'NONE',  ( 0.7071067811865487940, 0.7071067811865463515, 0.000000000000000000 ) ) ;
#22639=DIRECTION ( 'NONE',  ( -0.7071067811865486830, 0.7071067811865464625, 0.000000000000000000 ) ) ;
#22640=ORIENTED_EDGE ( 'NONE', *, *, #125985, .T. ) ;
#22641=ORIENTED_EDGE ( 'NONE', *, *, #79714, .F. ) ;
#22643=FACE_OUTER_BOUND ( 'NONE', #32085, .T. ) ;
#22644=CARTESIAN_POINT ( 'NONE',  ( 17.99999999999988276, -16.44781430457067373, 5.000000000000000000 ) ) ;
#22645=ORIENTED_EDGE ( 'NONE', *, *, #92410, .F. ) ;
#22647=EDGE_CURVE ( 'NONE', #140847, #95118, #47170, .T. ) ;
#22648=LINE ( 'NONE', #45894, #44597 ) ;
#22650=VERTEX_POINT ( 'NONE', #18727 ) ;
#22651=DIRECTION ( 'NONE',  ( 1.000000000000000000, 0.000000000000000000, 0.000000000000000000 ) ) ;
#22653=VERTEX_POINT ( 'NONE', #7119 ) ;
#22654=DIRECTION ( 'NONE',  ( 1.000000000000000000, 0.000000000000000000, 0.000000000000000000 ) ) ;
#22655=PLANE ( 'NONE',  #40770 ) ;
#22658=FACE_OUTER_BOUND ( 'NONE', #20577, .T. ) ;
#22659=ORIENTED_EDGE ( 'NONE', *, *, #123635, .T. ) ;
#22660=DIRECTION ( 'NONE',  ( 0.7071067811865486830, -0.7071067811865464625, -0.000000000000000000 ) ) ;
#22661=EDGE_LOOP ( 'NONE', ( #41402, #43038, #130511, #115633 ) ) ;
#22663=DIRECTION ( 'NONE',  ( -0.000000000000000000, 0.000000000000000000, 1.000000000000000000 ) ) ;
#22664=DIRECTION ( 'NONE',  ( -0.000000000000000000, -0.3543493200069152693, 0.9351131265310292928 ) ) ;
#22665=LINE ( 'NONE', #21981, #111685 ) ;
#22666=LINE ( 'NONE', #98139, #118083 ) ;
#22669=ORIENTED_EDGE ( 'NONE', *, *, #48260, .T. ) ;
#22672=EDGE_CURVE ( 'NONE', #38343, #97996, #62277, .T. ) ;
#22673=LINE ( 'NONE', #67689, #115802 ) ;
#22674=DIRECTION ( 'NONE',  ( -0.7071067811865486830, -0.7071067811865464625, -0.000000000000000000 ) ) ;
#22675=DIRECTION ( 'NONE',  ( -0.6830127018922180770, -0.6830127018922204085, -0.2588190451025213501 ) ) ;
#22676=ORIENTED_EDGE ( 'NONE', *, *, #91169, .T. ) ;
#22677=DIRECTION ( 'NONE',  ( 0.7071067811865487940, -0.7071067811865463515, 0.000000000000000000 ) ) ;
#22678=ORIENTED_EDGE ( 'NONE', *, *, #75299, .T. ) ;
#22680=EDGE_CURVE ( 'NONE', #49245, #42277, #128246, .T. ) ;
#22682=VERTEX_POINT ( 'NONE', #82588 ) ;
#22683=LINE ( 'NONE', #45235, #95536 ) ;
#22684=PLANE ( 'NONE',  #3952 ) ;
#22686=CARTESIAN_POINT ( 'NONE',  ( 40.98012225071428105, -17.24070752338409562, 20.23474786156478089 ) ) ;
#22687=VECTOR ( 'NONE', #137222, 1000.000000000000000 ) ;
#22689=FACE_BOUND ( 'NONE', #71688, .T. ) ;
#22690=EDGE_CURVE ( 'NONE', #107445, #52778, #112802, .T. ) ;
#22691=CARTESIAN_POINT ( 'NONE',  ( 2.999999999999981792, -6.108550654416958992, -3.114665004254960845 ) ) ;
#22693=CARTESIAN_POINT ( 'NONE',  ( 75.18398860626899705, 28.73617430169839793, 5.000000000000000000 ) ) ;
#22694=LINE ( 'NONE', #12560, #15734 ) ;
#22695=EDGE_LOOP ( 'NONE', ( #84259, #140302, #39994, #16378 ) ) ;
#22697=VECTOR ( 'NONE', #121684, 1000.000000000000000 ) ;
#22698=FACE_OUTER_BOUND ( 'NONE', #25280, .T. ) ;
#22699=ADVANCED_FACE ( 'NONE', ( #28921 ), #63007, .F. ) ;
#22700=ORIENTED_EDGE ( 'NONE', *, *, #17630, .F. ) ;
#22703=ORIENTED_EDGE ( 'NONE', *, *, #83532, .F. ) ;
#22704=DIRECTION ( 'NONE',  ( -0.6830127018922180770, -0.6830127018922204085, -0.2588190451025213501 ) ) ;
#22706=VERTEX_POINT ( 'NONE', #73161 ) ;
#22707=LINE ( 'NONE', #11120, #44424 ) ;
#22708=EDGE_CURVE ( 'NONE', #2860, #124916, #118023, .T. ) ;
#22709=DIRECTION ( 'NONE',  ( -0.7071067811865487940, 0.7071067811865463515, 0.000000000000000000 ) ) ;
#22710=LINE ( 'NONE', #100325, #90079 ) ;
#22711=CARTESIAN_POINT ( 'NONE',  ( 30.70710678118632941, 5.259292476615665457, 5.000000000000000000 ) ) ;
#22712=DIRECTION ( 'NONE',  ( 0.3543493200069163240, -0.000000000000000000, -0.9351131265310288487 ) ) ;
#22713=CARTESIAN_POINT ( 'NONE',  ( 14.99999999999989519, -15.41253812416060143, 4.000000000000000000 ) ) ;
#22715=DIRECTION ( 'NONE',  ( 0.7071067811865486830, -0.7071067811865464625, -0.000000000000000000 ) ) ;
#22716=PLANE ( 'NONE',  #60201 ) ;
#22717=VERTEX_POINT ( 'NONE', #138394 ) ;
#22718=EDGE_CURVE ( 'NONE', #76267, #104640, #41208, .T. ) ;
#22720=VERTEX_POINT ( 'NONE', #128937 ) ;
#22721=DIRECTION ( 'NONE',  ( 0.7071067811865486830, -0.7071067811865464625, -0.000000000000000000 ) ) ;
#22722=LINE ( 'NONE', #122788, #67541 ) ;
#22724=VECTOR ( 'NONE', #126739, 1000.000000000000000 ) ;
#22725=ORIENTED_EDGE ( 'NONE', *, *, #100152, .F. ) ;
#22726=VECTOR ( 'NONE', #128336, 1000.000000000000000 ) ;
#22727=ORIENTED_EDGE ( 'NONE', *, *, #129548, .T. ) ;
#22728=DIRECTION ( 'NONE',  ( 0.6830127018922180770, -0.6830127018922204085, -0.2588190451025213501 ) ) ;
#22729=ADVANCED_FACE ( 'NONE', ( #38374 ), #61581, .F. ) ;
#22730=ORIENTED_EDGE ( 'NONE', *, *, #14629, .T. ) ;
#22731=DIRECTION ( 'NONE',  ( -0.7071067811865486830, -0.7071067811865464625, -0.000000000000000000 ) ) ;
#22732=ADVANCED_FACE ( 'NONE', ( #27468 ), #29610, .F. ) ;
#22733=DIRECTION ( 'NONE',  ( -0.7071067811865486830, -0.7071067811865464625, 0.000000000000000000 ) ) ;
#22735=DIRECTION ( 'NONE',  ( -0.7071067811865487940, 0.7071067811865463515, -0.000000000000000000 ) ) ;
#22736=ORIENTED_EDGE ( 'NONE', *, *, #9737, .T. ) ;
#22737=PLANE ( 'NONE',  #96616 ) ;
#22738=LINE ( 'NONE', #111191, #30270 ) ;
#22739=DIRECTION ( 'NONE',  ( 0.7071067811865487940, -0.7071067811865463515, 0.000000000000000000 ) ) ;
#22740=CARTESIAN_POINT ( 'NONE',  ( 28.73493329717932099, 12.75929247661559351, 18.34774599283949570 ) ) ;
#22741=EDGE_LOOP ( 'NONE', ( #117758, #57753, #96799, #78039 ) ) ;
#22743=CARTESIAN_POINT ( 'NONE',  ( -23.99999999999983302, -16.60178936734450517, 0.8616154019346934367 ) ) ;
#22744=CARTESIAN_POINT ( 'NONE',  ( -29.99999999999978684, 20.96639925780205616, 5.000000000000000000 ) ) ;
#22745=DIRECTION ( 'NONE',  ( 0.3543493200069162685, -0.000000000000000000, -0.9351131265310288487 ) ) ;
#22746=ORIENTED_EDGE ( 'NONE', *, *, #102383, .F. ) ;
#22747=CARTESIAN_POINT ( 'NONE',  ( -13.49999999999989342, -20.94781430457062754, 5.000000000000000000 ) ) ;
#22748=CARTESIAN_POINT ( 'NONE',  ( 34.42499999999998295, -15.02281430457044742, 5.000000000000000000 ) ) ;
#22749=VERTEX_POINT ( 'NONE', #140518 ) ;
#22750=ADVANCED_FACE ( 'NONE', ( #105045 ), #51400, .F. ) ;
#22751=CARTESIAN_POINT ( 'NONE',  ( 0.000000000000000000, 0.000000000000000000, 5.000000000000000000 ) ) ;
#22752=LINE ( 'NONE', #97484, #136465 ) ;
#22754=DIRECTION ( 'NONE',  ( -0.6830127018922180770, -0.6830127018922204085, -0.2588190451025213501 ) ) ;
#22755=PLANE ( 'NONE',  #47127 ) ;
#22756=CARTESIAN_POINT ( 'NONE',  ( 8.510786437626906675, -27.52281430457049183, 5.000000000000000000 ) ) ;
#22758=EDGE_CURVE ( 'NONE', #20875, #84665, #49975, .T. ) ;
#22760=ORIENTED_EDGE ( 'NONE', *, *, #57288, .T. ) ;
#22761=LINE ( 'NONE', #25654, #35532 ) ;
#22762=CARTESIAN_POINT ( 'NONE',  ( 10.82816939922345689, 15.75929247661555799, 4.000000000000000000 ) ) ;
#22763=ORIENTED_EDGE ( 'NONE', *, *, #118800, .F. ) ;
#22764=FACE_OUTER_BOUND ( 'NONE', #2048, .T. ) ;
#22765=PLANE ( 'NONE',  #37208 ) ;
#22766=FACE_OUTER_BOUND ( 'NONE', #10827, .T. ) ;
#22767=VERTEX_POINT ( 'NONE', #126784 ) ;
#22768=CARTESIAN_POINT ( 'NONE',  ( -2.999999999999975575, -15.41253812416059787, 4.000000000000000000 ) ) ;
#22769=CARTESIAN_POINT ( 'NONE',  ( -57.48921356237308800, -27.52281430457095368, 5.000000000000000000 ) ) ;
#22772=CARTESIAN_POINT ( 'NONE',  ( 10.11017322888203651, -22.22500000000000853, 4.785647885939353863 ) ) ;
#22774=DIRECTION ( 'NONE',  ( -0.7071067811865486830, -0.7071067811865464625, 0.000000000000000000 ) ) ;
#22775=DIRECTION ( 'NONE',  ( 0.3543493200069162685, -0.000000000000000000, -0.9351131265310288487 ) ) ;
#22777=CARTESIAN_POINT ( 'NONE',  ( 80.99451991528748351, 28.92564299267994699, 4.000000000000000000 ) ) ;
#22778=EDGE_CURVE ( 'NONE', #70701, #71611, #72472, .T. ) ;
#22779=ORIENTED_EDGE ( 'NONE', *, *, #137503, .T. ) ;
#22780=EDGE_LOOP ( 'NONE', ( #43854, #77497, #92588, #50747 ) ) ;
#22781=CARTESIAN_POINT ( 'NONE',  ( -3.183988606268992161, 28.73617430169789699, 5.000000000000000000 ) ) ;
#22784=VECTOR ( 'NONE', #36183, 1000.000000000000000 ) ;
#22785=VECTOR ( 'NONE', #97979, 999.9999999999998863 ) ;
#22786=DIRECTION ( 'NONE',  ( -0.000000000000000000, 0.000000000000000000, 1.000000000000000000 ) ) ;
#22787=CARTESIAN_POINT ( 'NONE',  ( 60.18398860626900415, 28.73617430169829490, 5.000000000000000000 ) ) ;
#22788=VECTOR ( 'NONE', #59834, 1000.000000000000227 ) ;
#22790=EDGE_CURVE ( 'NONE', #33217, #66395, #71731, .T. ) ;
#22791=CARTESIAN_POINT ( 'NONE',  ( -66.48921356237309510, -27.52281430457101763, 5.000000000000000000 ) ) ;
#22792=DIRECTION ( 'NONE',  ( 1.000000000000000000, 0.000000000000000000, 0.000000000000000000 ) ) ;
#22793=ORIENTED_EDGE ( 'NONE', *, *, #124181, .T. ) ;
#22795=ORIENTED_EDGE ( 'NONE', *, *, #28799, .F. ) ;
#22799=VECTOR ( 'NONE', #73939, 1000.000000000000000 ) ;
#22800=AXIS2_PLACEMENT_3D ( 'NONE', #35871, #114787, #24936 ) ;
#22801=CARTESIAN_POINT ( 'NONE',  ( -28.82816939922332011, -14.24070752338413826, 4.000000000000000000 ) ) ;
#22804=DIRECTION ( 'NONE',  ( 0.6830127018922180770, -0.6830127018922204085, -0.2588190451025213501 ) ) ;
#22805=EDGE_CURVE ( 'NONE', #62799, #101394, #66551, .T. ) ;
#22806=CARTESIAN_POINT ( 'NONE',  ( 34.92499999999998295, 18.75929247661552779, 4.255531930566162302 ) ) ;
#22807=ORIENTED_EDGE ( 'NONE', *, *, #85201, .F. ) ;
#22809=ADVANCED_FACE ( 'NONE', ( #96982 ), #8537, .F. ) ;
#22811=LINE ( 'NONE', #95235, #78660 ) ;
#22812=FACE_OUTER_BOUND ( 'NONE', #30277, .T. ) ;
#22814=ORIENTED_EDGE ( 'NONE', *, *, #38822, .T. ) ;
#22817=ORIENTED_EDGE ( 'NONE', *, *, #8599, .T. ) ;
#22818=VECTOR ( 'NONE', #116983, 1000.000000000000000 ) ;
#22819=DIRECTION ( 'NONE',  ( -0.7071067811865486830, -0.7071067811865464625, 0.000000000000000000 ) ) ;
#22821=CARTESIAN_POINT ( 'NONE',  ( -63.18398860626900415, 28.73617430169831621, 5.000000000000000000 ) ) ;
#22823=ORIENTED_EDGE ( 'NONE', *, *, #84128, .T. ) ;
#22824=AXIS2_PLACEMENT_3D ( 'NONE', #60338, #36424, #105927 ) ;
#22825=DIRECTION ( 'NONE',  ( 0.3543493200069162685, -0.000000000000000000, -0.9351131265310288487 ) ) ;
#22826=VECTOR ( 'NONE', #49057, 1000.000000000000000 ) ;
#22827=CARTESIAN_POINT ( 'NONE',  ( 31.82816939922330235, -14.24070752338414714, 4.000000000000000000 ) ) ;
#22828=CARTESIAN_POINT ( 'NONE',  ( 38.99451991528749062, 28.92564299267965211, 4.000000000000000000 ) ) ;
#22830=DIRECTION ( 'NONE',  ( -0.000000000000000000, -0.3543493200069152693, 0.9351131265310292928 ) ) ;
#22831=DIRECTION ( 'NONE',  ( -0.7071067811865487940, 0.7071067811865463515, -0.000000000000000000 ) ) ;
#22833=ORIENTED_EDGE ( 'NONE', *, *, #803, .T. ) ;
#22834=LINE ( 'NONE', #90260, #53056 ) ;
#22835=LINE ( 'NONE', #43927, #112467 ) ;
#22837=AXIS2_PLACEMENT_3D ( 'NONE', #20309, #141395, #34087 ) ;
#22838=DIRECTION ( 'NONE',  ( 1.000000000000000000, -0.000000000000000000, 0.000000000000000000 ) ) ;
#22839=AXIS2_PLACEMENT_3D ( 'NONE', #5783, #50049, #98529 ) ;
#22840=ORIENTED_EDGE ( 'NONE', *, *, #41276, .T. ) ;
#22841=VERTEX_POINT ( 'NONE', #99138 ) ;
#22843=ADVANCED_FACE ( 'NONE', ( #142679 ), #21615, .F. ) ;
#22844=VERTEX_POINT ( 'NONE', #33930 ) ;
#22845=LINE ( 'NONE', #35935, #86979 ) ;
#22846=ADVANCED_FACE ( 'NONE', ( #43371 ), #131090, .F. ) ;
#22847=CARTESIAN_POINT ( 'NONE',  ( 2.510786437626908008, -27.52281430457053446, 5.000000000000000000 ) ) ;
#22848=CARTESIAN_POINT ( 'NONE',  ( -8.816011393731004731, 28.73617430169781173, 5.000000000000000000 ) ) ;
#22849=DIRECTION ( 'NONE',  ( -0.7071067811865486830, -0.7071067811865464625, 0.000000000000000000 ) ) ;
#22850=CARTESIAN_POINT ( 'NONE',  ( -1.499999999999994449, -10.91253812416063873, 4.000000000000000000 ) ) ;
#22851=VERTEX_POINT ( 'NONE', #110029 ) ;
#22853=VECTOR ( 'NONE', #24928, 1000.000000000000227 ) ;
#22856=EDGE_CURVE ( 'NONE', #114476, #15110, #31777, .T. ) ;
#22857=EDGE_CURVE ( 'NONE', #123401, #39039, #121617, .T. ) ;
#22859=CARTESIAN_POINT ( 'NONE',  ( -27.29974487139158512, -27.71228299555225405, 4.000000000000000000 ) ) ;
#22860=DIRECTION ( 'NONE',  ( 0.7071067811865487940, 0.7071067811865463515, 0.000000000000000000 ) ) ;
#22861=CARTESIAN_POINT ( 'NONE',  ( -24.29974487139158867, -27.71228299555223273, 4.000000000000000000 ) ) ;
#22862=ORIENTED_EDGE ( 'NONE', *, *, #64578, .T. ) ;
#22864=FACE_BOUND ( 'NONE', #18066, .T. ) ;
#22865=ADVANCED_FACE ( 'NONE', ( #110723 ), #89034, .T. ) ;
#22866=DIRECTION ( 'NONE',  ( -1.000000000000000000, 0.000000000000000000, 0.000000000000000000 ) ) ;
#22867=CARTESIAN_POINT ( 'NONE',  ( 54.48921356237310221, -27.52281430457093236, 5.000000000000000000 ) ) ;
#22868=CARTESIAN_POINT ( 'NONE',  ( -12.18398860626900060, 28.73617430169795739, 5.000000000000000000 ) ) ;
#22869=DIRECTION ( 'NONE',  ( -0.7071067811865487940, 0.7071067811865463515, 0.000000000000000000 ) ) ;
#22870=CARTESIAN_POINT ( 'NONE',  ( -39.48921356237310221, -27.52281430457082934, 5.000000000000000000 ) ) ;
#22871=ORIENTED_EDGE ( 'NONE', *, *, #100271, .F. ) ;
#22874=ORIENTED_EDGE ( 'NONE', *, *, #10903, .F. ) ;
#22875=EDGE_CURVE ( 'NONE', #47092, #142281, #54277, .T. ) ;
#22876=VERTEX_POINT ( 'NONE', #41948 ) ;
#22877=DIRECTION ( 'NONE',  ( -0.6830127018922181881, 0.6830127018922202975, -0.2588190451025214056 ) ) ;
#22878=EDGE_CURVE ( 'NONE', #28630, #32044, #107870, .T. ) ;
#22880=CARTESIAN_POINT ( 'NONE',  ( 36.48921356237310221, -27.52281430457080802, 5.000000000000000000 ) ) ;
#22881=VERTEX_POINT ( 'NONE', #44091 ) ;
#22884=VECTOR ( 'NONE', #42801, 1000.000000000000114 ) ;
#22885=CARTESIAN_POINT ( 'NONE',  ( 8.999999999999936051, 4.931123077392133069, 4.000000000000000000 ) ) ;
#22887=DIRECTION ( 'NONE',  ( -0.3543493200069162685, -0.000000000000000000, -0.9351131265310288487 ) ) ;
#22888=LINE ( 'NONE', #1148, #122226 ) ;
#22889=LINE ( 'NONE', #89607, #113262 ) ;
#22891=VECTOR ( 'NONE', #104014, 999.9999999999998863 ) ;
#22892=VECTOR ( 'NONE', #108345, 1000.000000000000000 ) ;
#22893=CARTESIAN_POINT ( 'NONE',  ( -23.99999999999982947, -0.1606350220013114671, 4.664761815935120737 ) ) ;
#22894=AXIS2_PLACEMENT_3D ( 'NONE', #99715, #34473, #142534 ) ;
#22896=LINE ( 'NONE', #101198, #88967 ) ;
#22897=CARTESIAN_POINT ( 'NONE',  ( 6.183988606268994381, 28.73617430169791476, 5.000000000000000000 ) ) ;
#22899=EDGE_LOOP ( 'NONE', ( #80732, #129564, #133346, #101136 ) ) ;
#22900=VERTEX_POINT ( 'NONE', #86163 ) ;
#22901=ORIENTED_EDGE ( 'NONE', *, *, #55192, .F. ) ;
#22903=ORIENTED_EDGE ( 'NONE', *, *, #89062, .T. ) ;
#22904=VECTOR ( 'NONE', #103738, 1000.000000000000000 ) ;
#22909=DIRECTION ( 'NONE',  ( 0.3543493200069164351, 2.781805975412904658E-17, -0.9351131265310288487 ) ) ;
#22910=ORIENTED_EDGE ( 'NONE', *, *, #57976, .T. ) ;
#22911=CARTESIAN_POINT ( 'NONE',  ( -16.49999999999988276, 12.05218569542904206, 5.000000000000000000 ) ) ;
#22912=VECTOR ( 'NONE', #21021, 1000.000000000000000 ) ;
#22913=CARTESIAN_POINT ( 'NONE',  ( 0.000000000000000000, 0.000000000000000000, 5.000000000000000000 ) ) ;
#22914=ORIENTED_EDGE ( 'NONE', *, *, #136476, .T. ) ;
#22915=DIRECTION ( 'NONE',  ( -1.000000000000000000, 0.000000000000000000, 0.000000000000000000 ) ) ;
#22916=DIRECTION ( 'NONE',  ( -0.3543493200069162685, -0.000000000000000000, -0.9351131265310288487 ) ) ;
#22917=ORIENTED_EDGE ( 'NONE', *, *, #126818, .T. ) ;
#22918=AXIS2_PLACEMENT_3D ( 'NONE', #65509, #19104, #108942 ) ;
#22919=CARTESIAN_POINT ( 'NONE',  ( -8.999999999999937828, 4.384688058510551656, -7.090945410444704500 ) ) ;
#22920=LINE ( 'NONE', #25992, #66050 ) ;
#22921=VERTEX_POINT ( 'NONE', #130386 ) ;
#22922=EDGE_LOOP ( 'NONE', ( #8284, #246, #33105, #38369 ) ) ;
#22923=ORIENTED_EDGE ( 'NONE', *, *, #109533, .T. ) ;
#22926=AXIS2_PLACEMENT_3D ( 'NONE', #46041, #57630, #3204 ) ;
#22927=LINE ( 'NONE', #54900, #5229 ) ;
#22928=VECTOR ( 'NONE', #88259, 1000.000000000000114 ) ;
#22929=CARTESIAN_POINT ( 'NONE',  ( 18.00548008471250583, 28.92564299267925776, 4.000000000000000000 ) ) ;
#22930=CARTESIAN_POINT ( 'NONE',  ( 0.000000000000000000, 0.000000000000000000, 5.000000000000000000 ) ) ;
#22931=VERTEX_POINT ( 'NONE', #63710 ) ;
#22936=CARTESIAN_POINT ( 'NONE',  ( -34.92500000000001137, 9.691175483027018700, 9.749534648445560947 ) ) ;
#22937=PLANE ( 'NONE',  #23527 ) ;
#22939=VERTEX_POINT ( 'NONE', #31079 ) ;
#22940=EDGE_CURVE ( 'NONE', #96370, #115757, #75297, .T. ) ;
#22941=ORIENTED_EDGE ( 'NONE', *, *, #30942, .F. ) ;
#22945=CARTESIAN_POINT ( 'NONE',  ( 3.183988606268992161, 28.73617430169789699, 5.000000000000000000 ) ) ;
#22946=PLANE ( 'NONE',  #36688 ) ;
#22949=LINE ( 'NONE', #100566, #131307 ) ;
#22950=CARTESIAN_POINT ( 'NONE',  ( 24.32816939922336630, -6.740707523384209310, 4.000000000000000000 ) ) ;
#22951=CARTESIAN_POINT ( 'NONE',  ( 8.994519915287490619, 28.92564299267944250, 4.000000000000000000 ) ) ;
#22952=ADVANCED_FACE ( 'NONE', ( #102030 ), #23759, .F. ) ;
#22953=ORIENTED_EDGE ( 'NONE', *, *, #86387, .T. ) ;
#22954=LINE ( 'NONE', #33887, #108909 ) ;
#22955=ORIENTED_EDGE ( 'NONE', *, *, #79193, .F. ) ;
#22958=ORIENTED_EDGE ( 'NONE', *, *, #52486, .F. ) ;
#22959=CARTESIAN_POINT ( 'NONE',  ( -14.99999999999989519, -6.033600742197674727, 5.000000000000000000 ) ) ;
#22960=LINE ( 'NONE', #67230, #97407 ) ;
#22961=VERTEX_POINT ( 'NONE', #124490 ) ;
#22963=DIRECTION ( 'NONE',  ( -0.7071067811865486830, -0.7071067811865464625, 0.000000000000000000 ) ) ;
#22964=DIRECTION ( 'NONE',  ( -0.7071067811865486830, -0.7071067811865464625, 0.000000000000000000 ) ) ;
#22965=ORIENTED_EDGE ( 'NONE', *, *, #134660, .T. ) ;
#22968=VERTEX_POINT ( 'NONE', #69418 ) ;
#22969=LINE ( 'NONE', #67236, #123222 ) ;
#22970=VERTEX_POINT ( 'NONE', #37502 ) ;
#22971=EDGE_CURVE ( 'NONE', #68934, #55692, #127640, .T. ) ;
#22972=CARTESIAN_POINT ( 'NONE',  ( -38.99451991528749062, 28.92564299267965211, 4.000000000000000000 ) ) ;
#22974=CARTESIAN_POINT ( 'NONE',  ( -14.99451991528749595, 28.92564299267948513, 4.000000000000000000 ) ) ;
#22975=EDGE_CURVE ( 'NONE', #46898, #88378, #112896, .T. ) ;
#22977=DIRECTION ( 'NONE',  ( 1.000000000000000000, 0.000000000000000000, 0.000000000000000000 ) ) ;
#22980=FACE_OUTER_BOUND ( 'NONE', #137132, .T. ) ;
#22981=DIRECTION ( 'NONE',  ( 0.6830127018922180770, -0.6830127018922204085, -0.2588190451025213501 ) ) ;
#22982=PLANE ( 'NONE',  #71007 ) ;
#22983=ORIENTED_EDGE ( 'NONE', *, *, #19739, .T. ) ;
#22984=ORIENTED_EDGE ( 'NONE', *, *, #64749, .F. ) ;
#22986=CARTESIAN_POINT ( 'NONE',  ( -34.92500000000001137, 0.006123077391933379188, 4.000000000000000000 ) ) ;
#22987=ORIENTED_EDGE ( 'NONE', *, *, #59123, .F. ) ;
#22989=FACE_OUTER_BOUND ( 'NONE', #108834, .T. ) ;
#22990=DIRECTION ( 'NONE',  ( 0.3543493200069162685, -0.000000000000000000, -0.9351131265310288487 ) ) ;
#22992=LINE ( 'NONE', #79617, #80321 ) ;
#22993=VERTEX_POINT ( 'NONE', #57839 ) ;
#22994=VECTOR ( 'NONE', #3144, 1000.000000000000000 ) ;
#22995=EDGE_CURVE ( 'NONE', #20866, #27961, #103428, .T. ) ;
#22996=VECTOR ( 'NONE', #13949, 999.9999999999998863 ) ;
#22997=CARTESIAN_POINT ( 'NONE',  ( -34.92500000000001137, 2.816654386410402555, 4.500000000000000888 ) ) ;
#22998=CARTESIAN_POINT ( 'NONE',  ( -34.49999999999975842, -13.53574439159936915, 4.994342998332166772 ) ) ;
#22999=VECTOR ( 'NONE', #125827, 1000.000000000000000 ) ;
#23000=FACE_OUTER_BOUND ( 'NONE', #124336, .T. ) ;
#23001=CARTESIAN_POINT ( 'NONE',  ( -48.48921356237309510, -27.52281430457089328, 5.000000000000000000 ) ) ;
#23003=LINE ( 'NONE', #10704, #28933 ) ;
#23004=ORIENTED_EDGE ( 'NONE', *, *, #73933, .F. ) ;
#23005=LINE ( 'NONE', #67278, #81662 ) ;
#23006=EDGE_CURVE ( 'NONE', #22717, #41095, #81004, .T. ) ;
#23007=LINE ( 'NONE', #58592, #1192 ) ;
#23009=EDGE_CURVE ( 'NONE', #67807, #88720, #113602, .T. ) ;
#23010=CARTESIAN_POINT ( 'NONE',  ( 24.79289321881329045, -2.240707523384254163, 5.000000000000000000 ) ) ;
#23011=AXIS2_PLACEMENT_3D ( 'NONE', #49250, #116614, #73136 ) ;
#23012=CARTESIAN_POINT ( 'NONE',  ( -50.99451991528749062, 28.92564299267973738, 4.000000000000000000 ) ) ;
#23014=ORIENTED_EDGE ( 'NONE', *, *, #91771, .F. ) ;
#23015=ORIENTED_EDGE ( 'NONE', *, *, #73615, .T. ) ;
#23019=DIRECTION ( 'NONE',  ( -0.6830127018922180770, -0.6830127018922204085, -0.2588190451025213501 ) ) ;
#23020=EDGE_CURVE ( 'NONE', #54370, #81280, #101309, .T. ) ;
#23022=LINE ( 'NONE', #67294, #41071 ) ;
#23024=VERTEX_POINT ( 'NONE', #1946 ) ;
#23025=DIRECTION ( 'NONE',  ( 0.7071067811865486830, -0.7071067811865464625, -0.000000000000000000 ) ) ;
#23026=PLANE ( 'NONE',  #21159 ) ;
#23027=EDGE_CURVE ( 'NONE', #62199, #127411, #142465, .T. ) ;
#23028=EDGE_CURVE ( 'NONE', #107481, #16142, #125209, .T. ) ;
#23029=LINE ( 'NONE', #45571, #39511 ) ;
#23030=VECTOR ( 'NONE', #73014, 1000.000000000000000 ) ;
#23032=ORIENTED_EDGE ( 'NONE', *, *, #45579, .T. ) ;
#23033=DIRECTION ( 'NONE',  ( 1.000000000000000000, -0.000000000000000000, -0.000000000000000000 ) ) ;
#23035=VECTOR ( 'NONE', #16831, 1000.000000000000227 ) ;
#23036=AXIS2_PLACEMENT_3D ( 'NONE', #89345, #142321, #132159 ) ;
#23039=VERTEX_POINT ( 'NONE', #106269 ) ;
#23041=CARTESIAN_POINT ( 'NONE',  ( 6.489213562373093325, -27.52281430457059841, 5.000000000000000000 ) ) ;
#23042=EDGE_CURVE ( 'NONE', #56720, #108519, #125932, .T. ) ;
#23045=VECTOR ( 'NONE', #35750, 1000.000000000000114 ) ;
#23047=CARTESIAN_POINT ( 'NONE',  ( 0.000000000000000000, 0.000000000000000000, 5.000000000000000000 ) ) ;
#23049=ORIENTED_EDGE ( 'NONE', *, *, #12363, .T. ) ;
#23050=EDGE_LOOP ( 'NONE', ( #90265, #143149, #23952, #10437 ) ) ;
#23051=EDGE_CURVE ( 'NONE', #94326, #62352, #104877, .T. ) ;
#23053=ORIENTED_EDGE ( 'NONE', *, *, #63175, .F. ) ;
#23054=ORIENTED_EDGE ( 'NONE', *, *, #94600, .T. ) ;
#23056=PLANE ( 'NONE',  #137746 ) ;
#23057=ORIENTED_EDGE ( 'NONE', *, *, #90365, .T. ) ;
#23058=DIRECTION ( 'NONE',  ( -0.7071067811865486830, -0.7071067811865464625, 0.000000000000000000 ) ) ;
#23060=CARTESIAN_POINT ( 'NONE',  ( 12.18398860626900060, 28.73617430169795739, 5.000000000000000000 ) ) ;
#23061=DIRECTION ( 'NONE',  ( -0.6830127018922181881, 0.6830127018922202975, -0.2588190451025214056 ) ) ;
#23063=VERTEX_POINT ( 'NONE', #116473 ) ;
#23065=ORIENTED_EDGE ( 'NONE', *, *, #25019, .T. ) ;
#23067=VERTEX_POINT ( 'NONE', #51231 ) ;
#23069=VERTEX_POINT ( 'NONE', #137520 ) ;
#23070=CARTESIAN_POINT ( 'NONE',  ( -45.29974487139158867, -27.71228299555237840, 4.000000000000000000 ) ) ;
#23072=EDGE_LOOP ( 'NONE', ( #96524, #110093, #87214, #94847 ) ) ;
#23073=ORIENTED_EDGE ( 'NONE', *, *, #136641, .F. ) ;
#23074=ADVANCED_FACE ( 'NONE', ( #7690 ), #40369, .F. ) ;
#23075=LINE ( 'NONE', #131883, #55895 ) ;
#23076=CARTESIAN_POINT ( 'NONE',  ( -35.99451991528749772, 28.92564299267963079, 4.000000000000000000 ) ) ;
#23077=LINE ( 'NONE', #102834, #88908 ) ;
#23079=FACE_OUTER_BOUND ( 'NONE', #59637, .T. ) ;
#23080=PLANE ( 'NONE',  #41292 ) ;
#23081=LINE ( 'NONE', #65228, #11136 ) ;
#23083=DIRECTION ( 'NONE',  ( 0.6830127018922181881, 0.6830127018922202975, -0.2588190451025214056 ) ) ;
#23084=ORIENTED_EDGE ( 'NONE', *, *, #23343, .F. ) ;
#23085=CARTESIAN_POINT ( 'NONE',  ( 25.49999999999982947, -16.91253812416058011, 4.000000000000000000 ) ) ;
#23086=LINE ( 'NONE', #48449, #119378 ) ;
#23087=CARTESIAN_POINT ( 'NONE',  ( -11.99999999999990585, -12.41253812416062985, 4.000000000000000000 ) ) ;
#23088=VERTEX_POINT ( 'NONE', #70850 ) ;
#23091=CARTESIAN_POINT ( 'NONE',  ( 2.999999999999975131, -10.77435723561695191, -9.972017380717238311 ) ) ;
#23092=VECTOR ( 'NONE', #102324, 999.9999999999998863 ) ;
#23093=AXIS2_PLACEMENT_3D ( 'NONE', #13496, #124426, #79554 ) ;
#23096=VECTOR ( 'NONE', #140953, 1000.000000000000000 ) ;
#23097=ORIENTED_EDGE ( 'NONE', *, *, #67451, .F. ) ;
#23098=CARTESIAN_POINT ( 'NONE',  ( 20.99999999999986144, 11.58746187583912324, 4.000000000000000000 ) ) ;
#23099=DIRECTION ( 'NONE',  ( -0.7071067811865487940, 0.7071067811865463515, 0.000000000000000000 ) ) ;
#23100=PLANE ( 'NONE',  #88942 ) ;
#23101=PLANE ( 'NONE',  #20939 ) ;
#23102=ORIENTED_EDGE ( 'NONE', *, *, #130098, .F. ) ;
#23104=VECTOR ( 'NONE', #42493, 1000.000000000000227 ) ;
#23106=LINE ( 'NONE', #80407, #531 ) ;
#23108=ORIENTED_EDGE ( 'NONE', *, *, #84922, .F. ) ;
#23110=CARTESIAN_POINT ( 'NONE',  ( -34.49999999999975131, -17.56887692260763956, 4.000000000000000000 ) ) ;
#23112=ORIENTED_EDGE ( 'NONE', *, *, #62804, .F. ) ;
#23113=VERTEX_POINT ( 'NONE', #51944 ) ;
#23115=DIRECTION ( 'NONE',  ( 0.7071067811865487940, -0.7071067811865463515, 0.000000000000000000 ) ) ;
#23116=AXIS2_PLACEMENT_3D ( 'NONE', #23357, #36397, #25497 ) ;
#23117=DIRECTION ( 'NONE',  ( -0.7071067811865486830, -0.7071067811865464625, 0.000000000000000000 ) ) ;
#23118=CARTESIAN_POINT ( 'NONE',  ( 0.000000000000000000, 0.000000000000000000, 5.000000000000000000 ) ) ;
#23119=CARTESIAN_POINT ( 'NONE',  ( 14.99451991528749595, 28.92564299267948513, 4.000000000000000000 ) ) ;
#23120=FACE_OUTER_BOUND ( 'NONE', #110235, .T. ) ;
#23121=VERTEX_POINT ( 'NONE', #93990 ) ;
#23124=EDGE_CURVE ( 'NONE', #83273, #26933, #117162, .T. ) ;
#23125=CARTESIAN_POINT ( 'NONE',  ( -0.005480084712502889671, 28.92564299267938210, 4.000000000000000000 ) ) ;
#23126=DIRECTION ( 'NONE',  ( 0.6830127018922180770, -0.6830127018922204085, -0.2588190451025213501 ) ) ;
#23127=EDGE_CURVE ( 'NONE', #86507, #88273, #27299, .T. ) ;
#23129=VERTEX_POINT ( 'NONE', #17162 ) ;
#23130=DIRECTION ( 'NONE',  ( 0.7071067811865487940, 0.7071067811865463515, 0.000000000000000000 ) ) ;
#23131=DIRECTION ( 'NONE',  ( -0.6830127018922180770, -0.6830127018922204085, -0.2588190451025213501 ) ) ;
#23132=VECTOR ( 'NONE', #41380, 1000.000000000000000 ) ;
#23133=ORIENTED_EDGE ( 'NONE', *, *, #133855, .F. ) ;
#23134=ADVANCED_FACE ( 'NONE', ( #18547 ), #28041, .T. ) ;
#23135=FACE_OUTER_BOUND ( 'NONE', #37640, .T. ) ;
#23136=VERTEX_POINT ( 'NONE', #41051 ) ;
#23137=ORIENTED_EDGE ( 'NONE', *, *, #42389, .F. ) ;
#23138=EDGE_CURVE ( 'NONE', #132741, #116545, #114999, .T. ) ;
#23139=EDGE_CURVE ( 'NONE', #101337, #1886, #59965, .T. ) ;
#23140=VECTOR ( 'NONE', #121635, 1000.000000000000000 ) ;
#23141=CARTESIAN_POINT ( 'NONE',  ( -14.38161509397995630, -2.240707523384260824, 13.37739548510242749 ) ) ;
#23142=VECTOR ( 'NONE', #55326, 1000.000000000000000 ) ;
#23143=FACE_OUTER_BOUND ( 'NONE', #141221, .T. ) ;
#23144=ORIENTED_EDGE ( 'NONE', *, *, #39848, .F. ) ;
#23145=CARTESIAN_POINT ( 'NONE',  ( 66.48921356237309510, -27.52281430457101763, 5.000000000000000000 ) ) ;
#23147=EDGE_CURVE ( 'NONE', #101509, #92497, #38913, .T. ) ;
#23148=EDGE_CURVE ( 'NONE', #103780, #3304, #72306, .T. ) ;
#23149=FACE_OUTER_BOUND ( 'NONE', #114739, .T. ) ;
#23151=DIRECTION ( 'NONE',  ( 1.000000000000000000, 0.000000000000000000, 0.000000000000000000 ) ) ;
#23153=CARTESIAN_POINT ( 'NONE',  ( 2.816011393730999401, 28.73617430169785436, 5.000000000000000000 ) ) ;
#23154=DIRECTION ( 'NONE',  ( 0.6830127018922180770, -0.6830127018922204085, -0.2588190451025213501 ) ) ;
#23155=EDGE_CURVE ( 'NONE', #74550, #34938, #83135, .T. ) ;
#23156=CARTESIAN_POINT ( 'NONE',  ( 17.81601139373099940, 28.73617430169775133, 5.000000000000000000 ) ) ;
#23157=DIRECTION ( 'NONE',  ( 0.7071067811865486830, -0.7071067811865464625, -0.000000000000000000 ) ) ;
#23158=PLANE ( 'NONE',  #27510 ) ;
#23160=VECTOR ( 'NONE', #53896, 1000.000000000000000 ) ;
#23162=CARTESIAN_POINT ( 'NONE',  ( -19.05000000000000071, 3.174999999999997158, 0.000000000000000000 ) ) ;
#23164=PLANE ( 'NONE',  #77825 ) ;
#23165=VERTEX_POINT ( 'NONE', #28763 ) ;
#23166=ORIENTED_EDGE ( 'NONE', *, *, #75569, .F. ) ;
#23169=EDGE_LOOP ( 'NONE', ( #77960, #58458, #75038, #82049 ) ) ;
#23172=CARTESIAN_POINT ( 'NONE',  ( 3.299744871391591339, -27.71228299555208352, 4.000000000000000000 ) ) ;
#23173=DIRECTION ( 'NONE',  ( -0.7071067811865486830, 0.7071067811865464625, 0.000000000000000000 ) ) ;
#23174=VECTOR ( 'NONE', #67745, 1000.000000000000000 ) ;
#23176=VERTEX_POINT ( 'NONE', #54111 ) ;
#23177=DIRECTION ( 'NONE',  ( 0.3543493200069162685, -0.000000000000000000, -0.9351131265310288487 ) ) ;
#23178=LINE ( 'NONE', #80471, #76572 ) ;
#23179=DIRECTION ( 'NONE',  ( 0.6830127018922180770, -0.6830127018922204085, -0.2588190451025213501 ) ) ;
#23180=ORIENTED_EDGE ( 'NONE', *, *, #129461, .F. ) ;
#23182=LINE ( 'NONE', #123272, #86698 ) ;
#23183=CARTESIAN_POINT ( 'NONE',  ( 32.18753812416031224, -22.22500000000000142, 4.000000000000000000 ) ) ;
#23184=EDGE_CURVE ( 'NONE', #68994, #129006, #131640, .T. ) ;
#23185=DIRECTION ( 'NONE',  ( -0.7071067811865487940, 0.7071067811865463515, 0.000000000000000000 ) ) ;
#23186=AXIS2_PLACEMENT_3D ( 'NONE', #38882, #59244, #106242 ) ;
#23188=LINE ( 'NONE', #26086, #105517 ) ;
#23189=CLOSED_SHELL ( 'NONE', ( #137798, #11692, #104368, #45731, #100110, #8352, #14703, #25783, #51710, #103740, #11894, #92745, #16823, #137321, #79630, #134169, #40307, #125559, #67396, #9068, #3197, #129681, #103579, #98799, #37983, #19569, #107477, #84254, #19901, #53463, #113555, #27937, #133919, #21845, #63546, #22024, #29646, #21954, #140473, #142697, #119004, #46534, #6057, #33935, #87011, #118981, #85619, #65659, #47955, #121513, #100649, #97828, #135757, #26954, #139418, #50673, #63932, #60469, #63042, #98236, #7337, #32686, #93114, #24209, #54145, #89178, #126437, #136590, #85296, #49188, #113335, #67253, #53506, #79120, #38240, #127478, #71703, #126664, #13841, #86902, #47980, #112944, #101907, #67390, #126988, #41661, #43653, #84133, #54431, #71218, #82724, #107695, #96883, #100043, #50891, #31601, #18662, #104134, #96064, #34683, #45477, #41188, #141355, #106102, #101431, #73909, #102651, #55180, #60721, #142224, #68439, #8866, #112362, #117843, #111602, #107454, #112826, #67884, #68156, #57544, #128145, #79090, #69774, #60906, #67202, #122774, #42543, #113197, #138443, #68728, #137325, #99743, #137026, #2629, #120918, #43461, #121057, #73641, #18126, #54665, #51331, #24583, #1325, #38417, #15239, #36998, #116105, #126268, #8918, #92076, #19006, #126348, #140556, #24359, #129391, #113413, #63511, #43668, #38809, #81807, #104288, #105630, #110083, #117766, #112876, #86064, #82611, #141582, #113101, #47822, #33290, #20135, #82138, #101917, #49174, #51328, #86887, #12527, #72720, #29715, #15769, #52512, #125203, #29272, #58968, #15578, #14202, #88301, #42028, #14463, #91201, #46152, #34128, #88822, #95151, #29557, #14698, #6395, #108026, #4303, #46173, #67125, #34139, #42594, #32227, #80525, #128249, #74586, #16570, #4484, #139672, #114582, #22561, #68029, #114826, #49063, #70211, #27065, #130048, #129873, #57166, #76602, #135346, #356, #117976, #26320, #129376, #72830, #34846, #36149, #7170, #123257, #68845, #130256, #88767, #80559, #77664, #61878, #98736, #38249, #129254, #104510, #12536, #46068, #26775, #69232, #39259, #10624, #129431, #30936, #90985, #113593, #62179, #74881, #86762, #49489, #106061, #76012, #93551, #100794, #26877, #135677, #101236, #80646, #65053, #37495, #100808, #60292, #44673, #2229, #4442, #24062, #3634, #27486, #135651, #17889, #82020, #29378, #114840, #78706, #119103, #63381, #62140, #95570, #105380, #138772, #67588, #77407, #38817, #123068, #73805, #93500, #98206, #70398, #104078, #134090, #38233, #4613, #55293, #99270, #44517, #93416, #106816, #124341, #34077, #57565, #63585, #109088, #38734, #109398, #2766, #139929, #109540, #128460, #39419, #56199, #124867, #3504, #31660, #75583, #18404, #104154, #133716, #27997, #134118, #110608, #7447, #68425, #132104, #109619, #58928, #32060, #73478, #87577, #69085, #130277, #43099, #129021, #33314, #112095, #80387, #67290, #95053, #4211, #103066, #75906, #6848, #64183, #125017, #10974, #58783, #34831, #51403, #35181, #101885, #4024, #5653, #127596, #82271, #118245, #59463, #55309, #113540, #74339, #57327, #92096, #9637, #24528, #122722, #70065, #17207, #112972, #90957, #72516, #3563, #122534, #90451, #82005, #96611, #80807, #18939, #35997, #45512, #106354, #136154, #25474, #63082, #100561, #84194, #62394, #106880, #111482, #63422, #19562, #48134, #5344, #71333, #85253, #23767, #137738, #49368, #103328, #17144, #82479, #3646, #139499, #104682, #48407, #97848, #70551, #79019, #31742, #96472, #47037, #85853, #78124, #32203, #140652, #9794, #125609, #121541, #58565, #130408, #32016, #119247, #133182, #126811, #36984, #88209, #117902, #62854, #32323, #60771, #78079, #130248, #116355, #4175, #109105, #28158, #25235, #92204, #21494, #58639, #59831, #41460, #65245, #117190, #77129, #16481, #14213, #59716, #94236, #31931, #85532, #90051, #87035, #45468, #66824, #140256, #127192, #89818, #66997, #71227, #64618, #81518, #68162, #111450, #94722, #124965, #94778, #123388, #126507, #23845, #69371, #128164, #19979, #97546, #6809, #129316, #44554, #77729, #64748, #14692, #69851, #26329, #126029, #88185, #104, #47187, #85230, #124167, #74524, #131373, #137510, #124356, #38416, #64116, #131748, #120047, #77400, #75558, #16015, #119123, #113701, #87144, #49886, #38531, #21545, #11906, #138246, #91040, #78883, #55630, #131689, #11542, #77104, #66556, #91019, #19695, #5209, #122818, #63501, #108102, #37713, #96299, #21554, #118500, #137117, #17493, #101147, #134047, #14529, #58104, #93411, #22150, #117256, #142814, #45552, #133573, #99219, #109077, #127461, #58602, #46759, #45847, #76433, #80347, #74500, #16795, #1123, #68396, #100836, #34494, #140394, #80002, #96552, #70889, #33833, #65322, #76156, #68749, #78426, #61113, #130531, #32835, #35009, #32247, #104500, #41723, #126801, #123553, #47141, #17588, #50942, #28627, #109961, #80170, #141601, #119782, #126638, #99544, #124028, #42160, #37554, #59186, #111986, #24754, #47372, #109324, #95122, #81919, #72177, #109258, #120038, #38145, #42454, #4935, #40408, #105030, #24298, #6530, #85733, #78378, #126931, #54401, #84454, #111316, #6247, #9267, #121252, #112755, #41727, #104274, #89731, #84017, #87705, #55285, #81305, #63610, #93493, #111163, #124890, #7929, #23134, #48494, #16280, #10715, #20070, #32434, #107951, #109966, #100516, #84912, #28939, #91046, #68065, #69932, #32002, #105263, #10912, #87550, #84751, #83666, #1973, #57027, #129262, #8623, #135683, #25039, #30318, #122368, #126151, #52858, #30450, #52577, #41529, #108900, #2865, #3044, #99414, #23894, #5920, #111260, #37452, #28494, #103931, #9487, #41078, #52977, #23282, #53714, #1446, #24880, #90886, #28982, #134490, #36316, #136247, #33233, #59115, #113365, #68452, #115348, #22865, #119542, #43202, #120043, #45491, #1743, #127511, #85461, #137626, #13031, #19340, #119449, #2787, #19453, #126019, #66849, #118749, #79220, #68108, #112594, #56503, #86100, #58349, #45304, #15294, #67484, #129283, #122699, #51117, #45329, #143186, #31800, #39090, #75256, #119114, #57445, #124317, #113090, #112728, #111912, #36209, #41031, #21038, #101769, #35643, #5543, #116803, #100337, #64402, #136885, #12929, #55942, #138970, #10083, #6559, #9892, #133134, #51630, #141683, #29869, #123078, #70822, #36016, #100988, #29149, #91030, #85192, #3280, #15140, #49141, #90502, #30935, #22809, #142557, #69528, #80518, #140619, #100550, #129590, #19678, #122937, #76092, #22952, #74956, #61022, #128779, #54880, #29680, #116948, #128250, #129886, #14339, #116189, #69476, #37431, #130683, #99447, #122091, #76776, #75430, #24343, #73341, #84588, #101298, #2378, #95450, #43111, #30860, #82900, #119862, #95504, #137703, #134179, #88366, #21654, #29221, #110467, #42248, #12914, #55157, #17018, #125417, #42561, #42980, #93782, #6111, #110161, #36782, #103364, #32731, #26962, #37067, #117559, #79390, #41846, #4998, #22163, #109931, #80462, #12272, #60049, #84604, #82928, #1901, #22729, #133288, #78674, #57174, #101788, #31844, #92877, #90441, #59596, #101531, #45196, #91277, #53844, #56242, #39900, #3178, #106350, #53478, #57110, #90646, #71488, #88558, #24174, #89952, #62345, #33690, #28362, #102461, #4809, #134393, #12590, #724, #76758, #6019, #93897, #88081, #125972, #49842, #111738, #44427, #12232, #106907, #84084, #44792, #25922, #93071, #142216, #115447, #67604, #132262, #93118, #106894, #103444, #3530, #78097, #131166, #79009, #83127, #117149, #10428, #13872, #130092, #100730, #99730, #12783, #47592, #100737, #130631, #135175, #94447, #54684, #99354, #128771, #19922, #53039, #36336, #108506, #17664, #25523, #9420, #58815, #84192, #61059, #114477, #136263, #49336, #91328, #80372, #51038, #98480, #55531, #50875, #116257, #11887, #135456, #94965, #61891, #65605, #65857, #68165, #61414, #35992, #2971, #84403, #79700, #134947, #95244, #138600, #99281, #92592, #98128, #128951, #82315, #31326, #32726, #3940, #98250, #48443, #78352, #141902, #85750, #57106, #127651, #38256, #21559, #24800, #94887, #94343, #127955, #138760, #1405, #35397, #27280, #7271, #27968, #98401, #62728, #60197, #74668, #83407, #46687, #75649, #120210, #126171, #100288, #120135, #45823, #74237, #3450, #132077, #1047, #31639, #81211, #104196, #66445, #52516, #22068, #52647, #52821, #28295, #113270, #112254, #97385, #139174, #109805, #127669, #92336, #90141, #11798, #39791, #51879, #98004, #98305, #84134, #16108, #114607, #5846, #44318, #63329, #5762, #31202, #51638, #102178, #125799, #61047, #7533, #23857, #138140, #19731, #51212, #95880, #2894, #126648, #7278, #114034, #106516, #87677, #34901, #17049, #90841, #142653, #133367, #16672, #70217, #135334, #113255, #47201, #88998, #88865, #113721, #32739, #98971, #21896, #61014, #113307, #105896, #137309, #23875, #67481, #125839, #97645, #110237, #33059, #7021, #14152, #47656, #104957, #40130, #97672, #130237, #42629, #131455, #117208, #60836, #129222, #54852, #63975, #15311, #28425, #2493, #105134, #31713, #40627, #80654, #10275, #54309, #24183, #87835, #38063, #14193, #30663, #27657, #104384, #5120, #63291, #41171, #139719, #56545, #44860, #4153, #31417, #137428, #121681, #36323, #39361, #39071, #97616, #5988, #141261, #20107, #130868, #71979, #66189, #76452, #42883, #127250, #67978, #31023, #102717, #15216, #130381, #72822, #98179, #139051, #139113, #138279, #25155, #65450, #107288, #110748, #31282, #115693, #100172, #16093, #67748, #47836, #114055, #43695, #75690, #27845, #24552, #109812, #59530, #129412, #7348, #126608, #115054, #40242, #996, #131070, #64419, #117535, #11389, #136715, #117123, #103563, #30956, #89167, #141383, #8541, #47401, #106523, #42691, #50887, #3388, #119533, #53186, #105065, #135665, #61803, #1794, #139812, #78236, #60085, #50303, #104527, #87239, #139553, #46833, #63660, #49098, #1125, #83864, #8267, #43898, #62867, #109381, #906, #62438, #135179, #68742, #3714, #98364, #87999, #27323, #89975, #133270, #98937, #17154, #141604, #26472, #1895, #45939, #14827, #104216, #91160, #79384, #122521, #33728, #126419, #17862, #123419, #19589, #131743, #153, #64295, #90131, #93343, #126578, #115143, #1719, #28945, #20095, #93927, #117096, #96454, #50427, #2230, #121859, #126304, #19656, #141570, #29493, #134163, #106272, #37475, #70371, #53657, #115270, #68330, #85783, #64867, #106039, #10249, #81270, #19345, #14601, #8194, #65839, #42214, #128593, #5186, #37195, #90493, #124720, #126049, #75563, #117286, #94579, #120886, #70192, #102559, #69419, #19050, #138502, #24507, #34179, #112757, #25913, #29967, #89391, #96169, #6943, #61262, #35485, #103015, #87208, #46970, #5458, #100761, #94035, #82863, #109384, #10451, #10038, #116028, #76394, #137589, #107965, #70221, #4348, #13892, #28142, #124095, #95129, #130586, #112335, #64173, #74233, #134907, #59154, #70374, #24686, #124263, #43994, #140383, #126071, #2164, #79915, #123620, #133531, #124851, #130973, #3499, #129551, #92100, #117633, #5470, #3175, #28125, #52493, #135800, #110232, #87730, #125322, #32924, #18201, #132318, #14176, #46315, #81009, #112005, #20076, #33176, #76395, #69534, #143495, #33456, #20374, #8927, #106848, #89842, #97835, #142659, #4626, #131363, #75828, #7029, #138975, #31693, #24695, #138130, #26319, #55622, #132569, #45250, #7438, #105639, #108924, #115337, #37259, #127182, #99521, #96984, #116856, #133894, #119031, #125442, #105475, #37446, #39109, #64504, #15394, #64285, #130578, #61852, #72027, #111391, #100547, #106340, #21565, #25847, #12404, #29057, #136498, #109168, #97702, #12808, #17297, #34744, #25960, #62419, #137338, #100636, #64401, #38, #82123, #85068, #128676, #136012, #61359, #131193, #139886, #131214, #45386, #132657, #116136, #96862, #1587, #109278, #131303, #128480, #133797, #59574, #99970, #103587, #15283, #42944, #100467, #88632, #34365, #77041, #130759, #65231, #110857, #68747, #121522, #98695, #53968, #113580, #114367, #6933, #44937, #76514, #58113, #113502, #98354, #70253, #95711, #4201, #27697, #87502, #55273, #48795, #117949, #18960, #62918, #91440, #6438, #41307, #47869, #26174, #65475, #130473, #121518, #141167, #60756, #96387, #15036, #29636, #1425, #67287, #14337, #5671, #33393, #115516, #97309, #16879, #138123, #61633, #134961, #37503, #1310, #18731, #21198, #50776, #53034, #125182, #89324, #138293, #115935, #57100, #65895, #28936, #140819, #4556, #72251, #80491, #54888, #29478, #60987, #59102, #108720, #46325, #44016, #28477, #52053, #63509, #27586, #15284, #131051, #123097, #82327, #18252, #76410, #72354, #92998, #102921, #122553, #99302, #34808, #60, #7878, #137610, #112937, #779, #17809, #1081, #69907, #22750, #61644, #81679, #96352, #38448, #32256, #95041, #100670, #61352, #19111, #22033, #96643, #20205, #74172, #76146, #98970, #89991, #24345, #36966, #42740, #45191, #80257, #17684, #121715, #19060, #58283, #1065, #3, #67090, #55825, #107845, #39491, #78738, #106946, #99500, #110246, #111402, #16260, #123935, #23329, #1591, #45586, #6437, #132112, #19507, #123099, #112150, #29893, #140205, #69184, #133046, #119694, #23435, #17240, #51850, #22508, #10140, #74992, #133081, #38191, #89381, #86535, #86626, #87646, #134521, #68736, #124232, #83783, #10882, #25194, #114409, #54434, #98863, #96806, #141611, #80855, #84957, #114695, #101488, #77118, #89616, #118069, #127130, #83605, #94082, #87987, #5280, #28975, #108969, #54997, #100138, #35120, #78303, #87549, #104851, #90468, #2597, #84502, #107108, #80140, #137779, #102582, #104033, #16293, #8263, #50549, #100790, #91844, #25128, #141018, #139430, #66335, #125495, #10641, #50271, #39660, #116104, #85555, #86019, #52916, #50866, #56161, #541, #41572, #21099, #34533, #25669, #110931, #53102, #123943, #73985, #117743, #100684, #134471, #49784, #84827, #85317, #761, #9929, #138579, #87104, #58063, #141799, #18001, #120237, #83025, #59541, #22322, #132854, #124538, #109174, #92058, #73927, #114890, #2564, #67178, #118130, #61098, #129915, #71701, #65954, #122071, #140111, #49643, #106321, #119705, #18934, #62994, #109853, #24230, #21779, #94270, #68599, #11509, #1055, #101894, #122565, #97892, #69923, #59232, #2388, #54204, #47399, #44716, #78893, #73877, #51931, #43369, #9150, #78652, #107793, #116560, #95842, #48716, #11603, #63993, #40196, #125625, #61108, #39338, #129938, #85573, #125571, #28792, #61962, #22340, #47133, #110070, #28778, #25268, #120787, #93064, #50588, #123283, #127790, #141285, #39737, #18461, #100365, #102286, #140486, #103218, #55995, #15461, #133990, #49719, #82990, #78319, #28932, #89897, #45885, #122418, #50690, #21795, #133021, #56313, #111904, #4640, #26493, #54040, #121809, #128741, #65422, #4255, #35316, #70493, #72437, #14397, #70442, #85056, #57484, #15153, #98025, #35883, #66129, #109555, #14248, #139440, #96894, #127904, #7362, #74871, #3115, #81632, #32073, #32967, #123879, #42616, #135247, #114690, #7990, #119430, #23823, #141552, #100839, #15189, #139092, #120504, #78387, #130671, #105552, #56132, #35247, #140715, #9713, #54866, #37166, #138526, #2694, #49820, #99250, #121594, #11362, #42259, #76829, #73255, #30425, #122160, #92230, #24846, #125085, #91782, #137799, #133478, #52036, #31268, #103056, #66446, #15969, #13238, #93915, #32791, #53687, #8531, #66658, #67359, #26287, #35853, #20519, #116316, #73815, #50738, #120113, #32201, #30209, #142988, #37153, #128312, #58123, #1056, #40398, #117206, #114983, #12688, #67850, #4119, #109662, #124456, #22376, #67223, #133078, #16588, #25308, #104960, #73810, #40716, #108126, #55927, #66329, #2603, #68923, #118160, #18935, #136776, #63668, #115043, #130945, #27819, #27547, #141412, #133520, #30700, #56303, #134365, #126782, #140310, #141510, #143013, #114201, #54962, #81538, #142813, #20304, #18820, #10082, #3061, #37801, #9812, #27096, #90665, #106943, #47677, #65233, #134351, #118627, #127128, #121508, #90094, #41597, #108358, #49718, #48993, #78283, #130672, #114376, #3744, #72571, #125155, #131912, #27235, #16688, #17461, #128842, #127613, #7762, #67192, #25884, #40887, #107798, #1530, #129992, #83472, #46196, #117600, #106278, #61358, #17477, #84655, #31231, #33212, #137457, #60244, #57305, #51270, #86859, #27942, #51939, #118463, #120042, #35491, #74872, #77834, #31070, #69866, #4496, #40437, #66750, #84331, #136869, #23074, #110250, #134078, #80936, #20272, #4335, #44405, #30390, #61355, #3065, #131369, #42717, #118733, #4813, #105252, #132929, #35755, #29749, #41263, #143101, #70473, #116000, #122766, #56627, #20214, #30523, #103050, #75280, #139523, #127607, #84267, #64169, #42036, #111831, #32732, #27317, #78200, #103213, #4381, #136990, #119989, #51682, #116004, #81986, #110701, #71501, #82411, #49715, #68727, #86674, #105203, #129078, #140279, #55694, #105840, #32207, #117291, #19032, #54944, #74503, #80267, #79671, #2340, #113884, #100324, #79268, #114618, #83606, #94818, #2150, #94094, #50551, #26625, #22699, #118067, #128598, #14067, #75512, #29960, #32449, #120133, #47324, #15667, #65326, #109736, #102258, #115163, #135101, #127664, #134541, #18290, #84278, #38242, #60492, #45957, #116990, #77382, #28911, #5545, #143507, #141348, #23901, #136569, #109821, #78030, #124584, #106748, #424, #121923, #3381, #106199, #91211, #132090, #17151, #16459, #56311, #81894, #22263, #39722, #139047, #79464, #18098, #133206, #47417, #31508, #16655, #950, #48760, #51592, #30312, #32187, #128296, #78233, #65940, #121867, #32874, #56439, #139711, #79049, #6213, #93220, #88895, #115817, #69288, #6627, #107111, #91423, #139959, #30988, #38597, #76773, #38881, #115603, #103684, #114086, #64799, #70661, #141000, #18743, #71146, #29542, #103826, #4579, #138168, #33389, #16154, #21925, #74022, #114276, #112112, #87808, #63354, #28736, #17769, #97289, #11978, #102141, #85283, #81006, #46780, #48402, #1629, #114387, #142715, #98024, #57570, #83737, #91581, #5885, #36560, #39686, #45153, #44503, #110868, #119522, #128616, #25631, #32578, #71438, #39602, #1067, #90066, #44640, #82312, #47483, #26807, #76382, #131784, #79605, #133054, #17201, #123195, #127598, #13553, #62516, #57575, #78732, #64331, #67410, #59869, #18070, #131717, #57181, #118452, #122060, #45297, #28485, #115377, #49290, #82945, #93703, #7660, #75568, #100578, #105882, #112432, #62607, #722, #95109, #48149, #101352, #88847, #94072, #120823, #58777, #120865, #135583, #64970, #52659, #123777, #9362, #24814, #47344, #91368, #2898, #13222, #18330, #61196, #118502, #128795, #35839, #16603, #96676, #107324, #28599, #28301, #98960, #24884, #84714, #58945, #106693, #77159, #2698, #131553, #38082, #6804, #76048, #52589, #33847, #113354, #93225, #71348, #25680, #140741, #85705, #101092, #96379, #117468, #69074, #137967, #60075, #98506, #16961, #29945, #62232, #122382, #53903, #67573, #23455, #123735, #54266, #21812, #596, #43752, #95096, #9077, #14411, #10575, #140061, #120396, #24829, #45070, #127680, #44127, #39415, #55356, #101696, #51385, #25853, #5516, #73328, #71503, #47820, #139527, #79567, #124510, #74326, #56769, #17906, #38094, #32793, #77560, #112400, #60809, #97949, #30881, #29511, #91798, #74642, #135959, #5675, #85587, #122851, #101158, #63167, #5572, #66557, #36622, #134766, #29136, #122208, #25176, #129547, #69347, #41667, #42497, #123675, #53330, #18366, #108677, #40798, #96201, #33866, #52604, #6611, #99128, #35137, #5664, #98647, #85887, #110073, #45036, #95282, #34765, #115175, #45213, #82113, #29433, #115325, #119589, #35400, #63759, #141931, #114867, #117449, #26391, #132049, #75074, #105492, #490, #82981, #3085, #121278, #140994, #24822, #118586, #81821, #64302, #44772, #57922, #19730, #46109, #37787, #68098, #36499, #8160, #101069, #92569, #131179, #78927, #3527, #81359, #69891, #40017, #138212, #76626, #22420, #124682, #101815, #137596, #41137, #12846, #85858, #62335, #94191, #70565, #70994, #40235, #11283, #114178, #31870, #125357, #81075, #15320, #60831, #73446, #89690, #51568, #82476, #31718, #128297, #33240, #23912, #121583, #93292, #27764, #133970, #140135, #80330, #139822, #123200, #139548, #6320, #99818, #49263, #108956, #26222, #90880, #90198, #35515, #111248, #6165, #4624, #103508, #48572, #104561, #119566, #12441, #37568, #10303, #92774, #52133, #15811, #69281, #100896, #92459, #128673, #91653, #141360, #133024, #8340, #109363, #107649, #136954, #101618, #105771, #38704, #66971, #142574, #56153, #109978, #41023, #2042, #64370, #23202, #8579, #68262, #80210, #4465, #115799, #65003, #9951, #111864, #68103, #63840, #18777, #55647, #114990, #47926, #88188, #118412, #105757, #42966, #8642, #95722, #90534, #53749, #141750, #90087, #7685, #65682, #97177, #12399, #25311, #117896, #127773, #45763, #104611, #104793, #124346, #58775, #8783, #48758, #56218, #82445, #85521, #39172, #85966, #81464, #133547, #115329, #56124, #42058, #89858, #47228, #117260, #18532, #136081, #110534, #114324, #24721, #127808, #106990, #77554, #132188, #119252, #123305, #113211, #113688, #45313, #94500, #107497, #118491, #67416, #40140, #42582, #47077, #128748, #2012, #19545, #5592, #133981, #42678, #21750, #39245, #23267, #115161, #82217, #7369, #47932, #67614, #38027, #98905, #98747, #42859, #72541, #97491, #125859, #31095, #47846, #18283, #83918, #98986, #17307, #31785, #81465, #82897, #74143, #120769, #43572, #80206, #54054, #133660, #87991, #106681, #98455, #81240, #5909, #14757, #106461, #136636, #136859, #2217, #67212, #30282, #29280, #36009, #40874, #45666, #37504, #67782, #96235, #51977, #10701, #29385, #99292, #51887, #17962, #74731, #81344, #9992, #138936, #77967, #54827, #137073, #66613, #130003, #115382, #24966, #53447, #29437, #86715, #55524, #34962, #25684, #16940, #93699, #40091, #2018, #103424, #125334, #27342, #111534, #931, #16456, #77470, #6178, #3400, #58423, #103416, #125380, #49878, #89976, #3142, #114261, #117990, #21732, #109584, #140808, #59952, #40361, #102180, #27419, #13357, #40243, #31566, #58317, #43523, #140196, #55774, #119177, #88530, #58985, #89450, #2086, #16463, #104181, #50860, #5038, #22217, #131741, #133725, #91429, #34033, #101095, #28588, #139364, #86646, #6818, #24043, #72759, #122175, #61522, #140538, #1318, #117342, #15804, #129183, #84576, #14093, #128239, #38423, #44811, #85108, #61829, #114186, #12657, #62148, #48988, #60069, #143005, #54349, #43248, #92974, #139248, #104856, #20532, #102884, #95525, #127462, #26045, #18865, #124278, #93805, #60178, #51104, #97694, #91281, #18946, #17244, #92598, #125029, #66463, #128834, #42906, #77757, #141921, #20920, #48399, #114497, #111473, #80408, #111357, #66955, #21518, #61442, #8604, #22582, #92136, #65294, #17528, #96846, #59663, #44754, #93682, #138588, #86797, #119528, #35367, #76082, #130501, #94210, #22046, #20268, #39535, #86479, #128925, #15192, #1681, #68137, #3082, #34122, #115002, #16130, #72670, #64933, #82697, #118908, #119256, #124971, #125794, #77502, #71683, #115646, #123838, #87186, #11746, #37934, #109087, #71809, #24731, #98687, #100483, #62830, #12549, #22843, #98492, #15124, #54409, #44747, #119793, #34390, #49501, #128149, #138424, #80117, #109303, #30990, #7457, #92874, #125129, #69621, #54969, #124699, #47627, #36648, #24562, #95475, #90473, #55977, #28147, #70104, #116892, #58292, #22054, #84938, #93723, #114328, #78657, #17904, #122388, #136597, #84149, #37627, #28360, #137679, #114673, #96533, #17510, #1117, #11721, #48551, #5313, #133830, #117916, #142040, #114664, #61254, #22456, #88363, #106605, #82773, #80425, #50230, #48077, #39697, #21436, #49201, #58881, #25676, #27399, #96554, #64313, #76108, #85260, #117953, #98064, #62194, #8753, #104121, #18163, #106084, #96969, #56330, #139766, #1842, #23438, #124005, #109499, #57320, #32866, #226, #35101, #85049, #31408, #102698, #83272, #50046, #13216, #45836, #84546, #63214, #112872, #76666, #55700, #93976, #11681, #66026, #137095, #16972, #37890, #50101, #77863, #26325, #127653, #5188, #64581, #7124, #31850, #75011, #133155, #142820, #95074, #127795, #37695, #101310, #103817, #61682, #23243, #5256, #136493, #62132, #134358, #118618, #39774, #31390, #13164, #136307, #123580, #30614, #138959, #71549, #133873, #40979, #58325, #84512, #119470, #12542, #76688, #29122, #83787, #67950, #9732, #9770, #37908, #92116, #142567, #98996, #87669, #75988, #72309, #116180, #54090, #108406, #133735, #121599, #4167, #105811, #37415, #107402, #126593, #73645, #12626, #98311, #76588, #44907, #55583, #86330, #52707, #42211, #135265, #90996, #76260, #45003, #40081, #9500, #143389, #75319, #132933, #30050, #135783, #135405, #44207, #121225, #22732, #1258, #58651, #5734, #2236, #83814, #39516, #110588, #86825, #81502, #37275, #104003, #41081, #49027, #86733, #87028, #29161, #38535, #10980, #78995, #129539, #122878, #141175, #84763, #4173, #30714, #6259, #57992, #10829, #85842, #135815, #106669, #21608, #5200, #6096, #77889, #50366, #60552, #109159, #65130, #133379, #129081, #137317, #27233, #55493, #41975, #49582, #13666, #3313, #101004, #84741, #33055, #101770, #110112, #33070, #41614, #70756, #20956, #109333, #94301, #79199, #87829, #12728, #4107, #132949, #53421, #37759, #78022, #63505, #119884, #8381, #83451, #43632, #61105, #86654, #116333, #70869, #55984, #125529, #13080, #66212, #97381, #63856, #11867, #8094, #12253, #83996, #35897, #136127, #80791, #45368, #42109, #29464, #138508, #140320, #130226, #86261, #58588, #105734, #125971, #54770, #73829, #49663, #121973, #121534, #132790, #136832, #142365, #134320, #31129, #105944, #47407, #56948, #2440, #87714, #22453, #122697, #69935, #3128, #31386, #37338, #82425, #5638, #90656, #129724, #57390, #94542, #133351, #19995, #47304, #142932, #130430, #58293, #48460, #69744, #57828, #123084, #43803, #106486, #8759, #54588, #82370, #128088, #66608, #104673, #50523, #93224, #2588, #124919, #15924, #28634, #27640, #59745, #66306, #6663, #103663, #54727, #18368, #112555, #24026, #120218, #41384, #64321, #54774, #29144, #36490, #26344, #9240, #135790, #139597, #117945, #100665, #142221, #10896, #127107, #22234, #36441, #140560, #138638, #56384, #65812, #126738, #51811, #122943, #93360, #96032, #110530, #78668, #12618, #13680, #75417, #134691, #107561, #139948, #62730, #85565, #101798, #86845, #15615, #80823, #35462, #72685, #90304, #138349, #38133, #121205, #92635, #90732, #62187, #108540, #127784, #114767, #46036, #31960, #132916, #66151, #141072, #141551, #23808, #71054, #65407, #63790, #56115, #82087, #26618, #65116, #75572, #71188, #77909, #89837, #142571, #6853, #30504, #85468, #12417, #30651, #73893, #45121, #1155, #78720, #10764, #15443, #132495, #119094, #124648, #8765, #135702, #134891, #55398, #28120, #105823, #28275, #61530, #54388, #102328, #92898, #8009, #140846, #50518, #113685, #130055, #92577, #99627, #9074, #20612, #52745, #19285, #88955, #15915, #43767, #28437, #51068, #67052, #96504, #74806, #2377, #107159, #104519, #140059, #135985, #32549, #60613, #45396, #117032, #73122, #24633, #107906, #97026, #81826, #73962, #15631, #18984, #126415, #114225, #60463, #37080, #53271, #6156, #6314, #124440, #100463, #28481, #75883, #36774, #85611, #86689, #123716, #39970, #25488, #83156, #84784, #86199, #115081, #41389, #22002, #71073, #31741, #104367, #75814, #142283, #76300, #36081, #116313, #95132, #119646, #72870, #34399, #47249, #87020, #126209, #65467, #51497, #83412, #29654, #7587, #2206, #55503, #85093, #82634, #107489, #89037, #21070, #114338, #123588, #111577, #86298, #109913, #109924, #68260, #62492, #70926, #6336, #61129, #126141, #51699, #37005, #49072, #131948, #133664, #80677, #15298, #121855, #35783, #26812, #109452, #66566, #92317, #110749, #42379, #64884, #36462, #8438, #97681, #66909, #13344, #62689, #41045, #103046, #57813, #142704, #51445, #56510, #87719, #136162, #88101, #78274, #6997, #82952, #95901, #60109, #123889, #18732, #132352, #80684, #15567, #96528, #65423, #110721, #69408, #75142, #82647, #61978, #139507, #7486, #13810, #91712, #62512, #44294, #33348, #96796, #48452, #27756, #12944, #2303, #98914, #34750, #8955, #42865, #55923, #9070, #143252, #30805, #66107, #140077, #8877, #90027, #34364, #51975, #3553, #45595, #98807, #93564, #68109, #100119, #68557, #24853, #100626, #137427, #89787, #139234, #28666, #49803, #53268, #99017, #5471, #108012, #6726, #87770, #31059, #10117, #39641, #52986, #74770, #83537, #129270, #105863, #11073, #104917, #8496, #50728, #64898, #105450, #6445, #35524, #15580, #26693, #27044, #22846, #30894, #3681, #129583, #115047, #38609, #108181, #4052, #113390, #39631, #17164, #83274, #46289, #41912, #101375, #118655, #18924, #104672, #79849, #139944, #28944, #90157, #59946, #52040, #24672, #41898, #136423, #63945, #102979, #119276, #74779, #41904, #15674, #5084, #106449, #3492, #98328, #114709, #59315, #86348, #56827, #5658, #18756, #137804, #97832, #111068, #83313, #119355, #86741, #40316, #84292, #56072, #55369, #97384, #47479, #25793, #105315, #40762, #23665, #69102, #39748, #111039, #80052, #114361, #8153, #95082, #3228, #82487, #63924, #97925, #112811, #60116, #55264, #140096, #10253, #38377, #94328, #26081, #125878, #66407, #74830, #74425, #22183, #51421, #119171, #65874, #22550, #106177, #8320, #67084, #79136, #84982, #119363, #130222, #63717, #73453, #48300, #66396, #101125, #139720, #92087, #109672, #21820, #83011, #90510, #106631, #138419, #4336, #23226, #57119, #18074, #68384, #50146, #128130, #33405, #113642, #78364, #87930, #118104, #134115, #71663, #135313, #88832, #35379, #69970, #21211, #136126, #115454, #81408, #35945, #96186, #139376, #131713, #123432, #27580, #112416, #15809, #37636, #71978, #32588, #2411, #11082, #99977, #100252, #104886, #117802, #57052, #54706, #51515, #76214, #32713, #90161, #7822, #56483, #76207, #119939, #114513, #30261, #141078, #39252, #1958, #138435, #128032, #7642, #25726, #134467, #133634, #13332, #51260, #8424, #84305, #97807, #26870, #36359, #45593, #111344, #140534, #68936, #26173, #38781 ) ) ;
#23192=EDGE_LOOP ( 'NONE', ( #6510, #60783, #68050, #126474, #95522, #20256 ) ) ;
#23193=ORIENTED_EDGE ( 'NONE', *, *, #69469, .T. ) ;
#23195=VERTEX_POINT ( 'NONE', #96816 ) ;
#23197=CARTESIAN_POINT ( 'NONE',  ( 9.183988606268997046, 28.73617430169793607, 5.000000000000000000 ) ) ;
#23199=LINE ( 'NONE', #45038, #109177 ) ;
#23200=LINE ( 'NONE', #108064, #102098 ) ;
#23201=VECTOR ( 'NONE', #17873, 1000.000000000000000 ) ;
#23202=ADVANCED_FACE ( 'NONE', ( #19299 ), #98297, .F. ) ;
#23203=AXIS2_PLACEMENT_3D ( 'NONE', #4903, #140457, #104237 ) ;
#23205=VERTEX_POINT ( 'NONE', #375 ) ;
#23206=EDGE_CURVE ( 'NONE', #59816, #86810, #109158, .T. ) ;
#23207=VERTEX_POINT ( 'NONE', #141063 ) ;
#23208=DIRECTION ( 'NONE',  ( 0.7071067811865486830, -0.7071067811865464625, -0.000000000000000000 ) ) ;
#23209=VECTOR ( 'NONE', #48458, 1000.000000000000000 ) ;
#23210=VECTOR ( 'NONE', #131222, 1000.000000000000000 ) ;
#23211=VECTOR ( 'NONE', #122271, 1000.000000000000227 ) ;
#23213=CARTESIAN_POINT ( 'NONE',  ( -12.70710678118644665, -9.740707523384180888, 5.000000000000000000 ) ) ;
#23214=EDGE_CURVE ( 'NONE', #8442, #22844, #132382, .T. ) ;
#23215=VECTOR ( 'NONE', #115084, 1000.000000000000000 ) ;
#23216=ORIENTED_EDGE ( 'NONE', *, *, #72244, .F. ) ;
#23219=VERTEX_POINT ( 'NONE', #87422 ) ;
#23223=EDGE_CURVE ( 'NONE', #102488, #124605, #142525, .T. ) ;
#23225=EDGE_LOOP ( 'NONE', ( #99212, #95349, #78138, #140570 ) ) ;
#23226=ADVANCED_FACE ( 'NONE', ( #21446 ), #110558, .F. ) ;
#23227=CARTESIAN_POINT ( 'NONE',  ( -29.29298673570674794, -21.74070752338405299, 4.999753212805210012 ) ) ;
#23228=VERTEX_POINT ( 'NONE', #108399 ) ;
#23229=ORIENTED_EDGE ( 'NONE', *, *, #43030, .F. ) ;
#23230=AXIS2_PLACEMENT_3D ( 'NONE', #4229, #4970, #92021 ) ;
#23231=VERTEX_POINT ( 'NONE', #86716 ) ;
#23232=AXIS2_PLACEMENT_3D ( 'NONE', #32539, #31119, #9296 ) ;
#23233=VECTOR ( 'NONE', #113856, 1000.000000000000000 ) ;
#23234=DIRECTION ( 'NONE',  ( -0.7071067811865486830, -0.7071067811865464625, 0.000000000000000000 ) ) ;
#23235=EDGE_CURVE ( 'NONE', #35520, #128274, #41772, .T. ) ;
#23236=ORIENTED_EDGE ( 'NONE', *, *, #101781, .F. ) ;
#23237=CARTESIAN_POINT ( 'NONE',  ( 33.48921356237309510, -27.52281430457078670, 5.000000000000000000 ) ) ;
#23238=VECTOR ( 'NONE', #51581, 1000.000000000000000 ) ;
#23241=VECTOR ( 'NONE', #42286, 999.9999999999998863 ) ;
#23242=LINE ( 'NONE', #131320, #130067 ) ;
#23243=ADVANCED_FACE ( 'NONE', ( #33076 ), #53347, .F. ) ;
#23244=FACE_BOUND ( 'NONE', #133518, .T. ) ;
#23245=VERTEX_POINT ( 'NONE', #8378 ) ;
#23246=CARTESIAN_POINT ( 'NONE',  ( 0.000000000000000000, 0.000000000000000000, 5.000000000000000000 ) ) ;
#23247=DIRECTION ( 'NONE',  ( -0.000000000000000000, 0.000000000000000000, 1.000000000000000000 ) ) ;
#23248=VECTOR ( 'NONE', #52739, 1000.000000000000000 ) ;
#23249=DIRECTION ( 'NONE',  ( -0.7071067811865487940, 0.7071067811865463515, 0.000000000000000000 ) ) ;
#23250=PLANE ( 'NONE',  #90210 ) ;
#23251=ORIENTED_EDGE ( 'NONE', *, *, #79310, .T. ) ;
#23253=VERTEX_POINT ( 'NONE', #22132 ) ;
#23254=ORIENTED_EDGE ( 'NONE', *, *, #89629, .T. ) ;
#23256=EDGE_CURVE ( 'NONE', #82657, #79834, #63556, .T. ) ;
#23260=DIRECTION ( 'NONE',  ( 0.6830127018922181881, 0.6830127018922202975, -0.2588190451025214056 ) ) ;
#23262=VERTEX_POINT ( 'NONE', #85251 ) ;
#23263=LINE ( 'NONE', #132073, #37574 ) ;
#23265=LINE ( 'NONE', #64, #138475 ) ;
#23267=ADVANCED_FACE ( 'NONE', ( #75140 ), #130219, .F. ) ;
#23270=CARTESIAN_POINT ( 'NONE',  ( -65.99451991528749772, 28.92564299267984396, 4.000000000000000000 ) ) ;
#23271=PLANE ( 'NONE',  #125791 ) ;
#23273=ORIENTED_EDGE ( 'NONE', *, *, #21916, .F. ) ;
#23274=VERTEX_POINT ( 'NONE', #74414 ) ;
#23275=VECTOR ( 'NONE', #67386, 1000.000000000000227 ) ;
#23276=ORIENTED_EDGE ( 'NONE', *, *, #87257, .F. ) ;
#23277=DIRECTION ( 'NONE',  ( -0.7071067811865487940, 0.7071067811865463515, -0.000000000000000000 ) ) ;
#23278=DIRECTION ( 'NONE',  ( 0.7071067811865487940, 0.7071067811865463515, 0.000000000000000000 ) ) ;
#23279=ORIENTED_EDGE ( 'NONE', *, *, #77901, .T. ) ;
#23280=VERTEX_POINT ( 'NONE', #119306 ) ;
#23282=ADVANCED_FACE ( 'NONE', ( #118602 ), #141814, .T. ) ;
#23283=LINE ( 'NONE', #22558, #122671 ) ;
#23284=ORIENTED_EDGE ( 'NONE', *, *, #106707, .T. ) ;
#23285=DIRECTION ( 'NONE',  ( -0.6830127018922181881, 0.6830127018922202975, -0.2588190451025214056 ) ) ;
#23286=VECTOR ( 'NONE', #90047, 1000.000000000000227 ) ;
#23288=CARTESIAN_POINT ( 'NONE',  ( 22.88901570796818774, -1.420450978533076558, 4.272001239691295638 ) ) ;
#23291=VERTEX_POINT ( 'NONE', #77976 ) ;
#23293=LINE ( 'NONE', #80577, #96199 ) ;
#23294=DIRECTION ( 'NONE',  ( -0.7071067811865486830, -0.7071067811865464625, 0.000000000000000000 ) ) ;
#23296=CARTESIAN_POINT ( 'NONE',  ( -45.29974487139158867, -27.71228299555237840, 4.000000000000000000 ) ) ;
#23297=DIRECTION ( 'NONE',  ( 0.7071067811865487940, -0.7071067811865463515, 0.000000000000000000 ) ) ;
#23298=ORIENTED_EDGE ( 'NONE', *, *, #64749, .T. ) ;
#23299=DIRECTION ( 'NONE',  ( 0.6830127018922180770, -0.6830127018922204085, -0.2588190451025213501 ) ) ;
#23300=ORIENTED_EDGE ( 'NONE', *, *, #120715, .T. ) ;
#23301=DIRECTION ( 'NONE',  ( -0.3543493200069163240, 0.000000000000000000, -0.9351131265310288487 ) ) ;
#23302=VECTOR ( 'NONE', #80580, 1000.000000000000000 ) ;
#23303=DIRECTION ( 'NONE',  ( 1.000000000000000000, 0.000000000000000000, 0.000000000000000000 ) ) ;
#23304=LINE ( 'NONE', #102345, #128202 ) ;
#23305=( BOUNDED_CURVE ( )  B_SPLINE_CURVE ( 3, ( #41392, #131267, #120344, #110204 ),
 .UNSPECIFIED., .F., .F. ) 
 B_SPLINE_CURVE_WITH_KNOTS ( ( 4, 4 ),
 ( 4.407062196515976638, 4.453802039120700940 ),
 .UNSPECIFIED. ) 
 CURVE ( )  GEOMETRIC_REPRESENTATION_ITEM ( )  RATIONAL_B_SPLINE_CURVE ( ( 1.000000000000000000, 0.9998179572116046021, 0.9998179572116046021, 1.000000000000000000 ) ) 
 REPRESENTATION_ITEM ( '' )  );
#23306=EDGE_LOOP ( 'NONE', ( #47, #64919, #117252, #122097 ) ) ;
#23307=VECTOR ( 'NONE', #10765, 1000.000000000000000 ) ;
#23308=VECTOR ( 'NONE', #32911, 999.9999999999998863 ) ;
#23309=CARTESIAN_POINT ( 'NONE',  ( -26.99451991528749417, 28.92564299267956685, 4.000000000000000000 ) ) ;
#23311=ORIENTED_EDGE ( 'NONE', *, *, #115035, .F. ) ;
#23312=VECTOR ( 'NONE', #13145, 999.9999999999998863 ) ;
#23313=VECTOR ( 'NONE', #17284, 1000.000000000000000 ) ;
#23314=VECTOR ( 'NONE', #62065, 1000.000000000000227 ) ;
#23315=VECTOR ( 'NONE', #20354, 1000.000000000000000 ) ;
#23316=( BOUNDED_CURVE ( )  B_SPLINE_CURVE ( 3, ( #68711, #71557, #102758, #81744 ),
 .UNSPECIFIED., .F., .T. ) 
 B_SPLINE_CURVE_WITH_KNOTS ( ( 4, 4 ),
 ( 5.920967161967927161, 7.341195215986642708 ),
 .UNSPECIFIED. ) 
 CURVE ( )  GEOMETRIC_REPRESENTATION_ITEM ( )  RATIONAL_B_SPLINE_CURVE ( ( 1.000000000000000000, 0.8388583629366603844, 0.8388583629366603844, 1.000000000000000000 ) ) 
 REPRESENTATION_ITEM ( '' )  );
#23317=DIRECTION ( 'NONE',  ( -0.7071067811865487940, 0.7071067811865463515, 0.000000000000000000 ) ) ;
#23318=VECTOR ( 'NONE', #65619, 1000.000000000000000 ) ;
#23319=VERTEX_POINT ( 'NONE', #48740 ) ;
#23320=CARTESIAN_POINT ( 'NONE',  ( 33.48921356237309510, -27.52281430457078670, 5.000000000000000000 ) ) ;
#23322=ORIENTED_EDGE ( 'NONE', *, *, #12154, .F. ) ;
#23323=EDGE_CURVE ( 'NONE', #111354, #15103, #136437, .T. ) ;
#23324=ORIENTED_EDGE ( 'NONE', *, *, #66320, .T. ) ;
#23327=CARTESIAN_POINT ( 'NONE',  ( -4.499999999999968914, 13.56627193232214523, -10.57019076586069772 ) ) ;
#23328=ORIENTED_EDGE ( 'NONE', *, *, #132683, .T. ) ;
#23329=ADVANCED_FACE ( 'NONE', ( #71217 ), #81391, .F. ) ;
#23330=DIRECTION ( 'NONE',  ( 0.7071067811865487940, 0.7071067811865463515, -0.000000000000000000 ) ) ;
#23331=EDGE_CURVE ( 'NONE', #45528, #114150, #100436, .T. ) ;
#23332=EDGE_CURVE ( 'NONE', #54652, #94433, #3750, .T. ) ;
#23333=CARTESIAN_POINT ( 'NONE',  ( 11.99451991528749417, 28.92564299267946382, 4.000000000000000000 ) ) ;
#23334=EDGE_CURVE ( 'NONE', #27882, #108415, #137179, .T. ) ;
#23335=EDGE_LOOP ( 'NONE', ( #116460, #90751, #101462, #119209 ) ) ;
#23337=FACE_OUTER_BOUND ( 'NONE', #135922, .T. ) ;
#23339=DIRECTION ( 'NONE',  ( 0.7071067811865487940, 0.7071067811865463515, 0.000000000000000000 ) ) ;
#23340=PLANE ( 'NONE',  #72554 ) ;
#23343=EDGE_CURVE ( 'NONE', #33303, #100766, #93669, .T. ) ;
#23347=AXIS2_PLACEMENT_3D ( 'NONE', #73391, #96510, #141486 ) ;
#23348=ORIENTED_EDGE ( 'NONE', *, *, #113999, .T. ) ;
#23349=ORIENTED_EDGE ( 'NONE', *, *, #130879, .F. ) ;
#23351=EDGE_CURVE ( 'NONE', #88704, #125103, #71940, .T. ) ;
#23352=AXIS2_PLACEMENT_3D ( 'NONE', #11074, #33608, #93494 ) ;
#23353=ORIENTED_EDGE ( 'NONE', *, *, #107961, .T. ) ;
#23354=ORIENTED_EDGE ( 'NONE', *, *, #103718, .T. ) ;
#23355=ORIENTED_EDGE ( 'NONE', *, *, #105669, .F. ) ;
#23357=CARTESIAN_POINT ( 'NONE',  ( -54.18398860626899705, 28.73617430169825226, 5.000000000000000000 ) ) ;
#23358=VECTOR ( 'NONE', #87902, 1000.000000000000227 ) ;
#23360=CARTESIAN_POINT ( 'NONE',  ( 48.18398860626899705, 28.73617430169820608, 5.000000000000000000 ) ) ;
#23361=CARTESIAN_POINT ( 'NONE',  ( -20.99451991528748707, 28.92564299267952777, 4.000000000000000000 ) ) ;
#23363=LINE ( 'NONE', #34995, #104182 ) ;
#23364=DIRECTION ( 'NONE',  ( -0.7071067811865487940, 0.7071067811865463515, -0.000000000000000000 ) ) ;
#23367=EDGE_LOOP ( 'NONE', ( #143116, #88131, #80266, #46485 ) ) ;
#23368=DIRECTION ( 'NONE',  ( -0.000000000000000000, -0.3543493200069152693, 0.9351131265310292928 ) ) ;
#23369=DIRECTION ( 'NONE',  ( 0.7071067811865487940, -0.7071067811865463515, 0.000000000000000000 ) ) ;
#23370=CARTESIAN_POINT ( 'NONE',  ( 19.82816939922339117, 9.759292476615614831, 4.000000000000000000 ) ) ;
#23371=CARTESIAN_POINT ( 'NONE',  ( 29.99451991528749417, 28.92564299267958816, 4.000000000000000000 ) ) ;
#23372=EDGE_CURVE ( 'NONE', #112760, #14379, #69808, .T. ) ;
#23376=DIRECTION ( 'NONE',  ( -0.000000000000000000, -0.3543493200069152693, 0.9351131265310292928 ) ) ;
#23377=DIRECTION ( 'NONE',  ( -0.3543493200069162685, -0.000000000000000000, -0.9351131265310288487 ) ) ;
#23378=AXIS2_PLACEMENT_3D ( 'NONE', #63597, #9880, #62874 ) ;
#23379=ORIENTED_EDGE ( 'NONE', *, *, #21397, .T. ) ;
#23380=EDGE_LOOP ( 'NONE', ( #142296, #68291, #9932, #116399 ) ) ;
#23382=FACE_OUTER_BOUND ( 'NONE', #13189, .T. ) ;
#23383=VECTOR ( 'NONE', #92550, 1000.000000000000000 ) ;
#23384=FACE_OUTER_BOUND ( 'NONE', #19910, .T. ) ;
#23385=ORIENTED_EDGE ( 'NONE', *, *, #899, .F. ) ;
#23386=AXIS2_PLACEMENT_3D ( 'NONE', #1900, #78815, #23706 ) ;
#23387=FACE_OUTER_BOUND ( 'NONE', #54695, .T. ) ;
#23388=CARTESIAN_POINT ( 'NONE',  ( 36.18398860626899705, 28.73617430169812437, 5.000000000000000000 ) ) ;
#23390=VERTEX_POINT ( 'NONE', #34458 ) ;
#23391=EDGE_CURVE ( 'NONE', #136547, #4967, #67096, .T. ) ;
#23396=LINE ( 'NONE', #113995, #133391 ) ;
#23398=EDGE_CURVE ( 'NONE', #68247, #61017, #78680, .T. ) ;
#23399=LINE ( 'NONE', #111862, #62601 ) ;
#23400=ORIENTED_EDGE ( 'NONE', *, *, #24979, .T. ) ;
#23401=LINE ( 'NONE', #88694, #44184 ) ;
#23403=LINE ( 'NONE', #113267, #58679 ) ;
#23404=DIRECTION ( 'NONE',  ( -0.7071067811865486830, -0.7071067811865464625, 0.000000000000000000 ) ) ;
#23405=PLANE ( 'NONE',  #19936 ) ;
#23407=PLANE ( 'NONE',  #129598 ) ;
#23408=VECTOR ( 'NONE', #36244, 1000.000000000000000 ) ;
#23409=LINE ( 'NONE', #45913, #48486 ) ;
#23410=EDGE_CURVE ( 'NONE', #1311, #83494, #28577, .T. ) ;
#23412=PLANE ( 'NONE',  #40740 ) ;
#23414=CARTESIAN_POINT ( 'NONE',  ( 4.828169399223495084, -2.240707523384264377, 4.000000000000000000 ) ) ;
#23416=FACE_OUTER_BOUND ( 'NONE', #7301, .T. ) ;
#23417=DIRECTION ( 'NONE',  ( 0.000000000000000000, -1.000000000000000000, 0.000000000000000000 ) ) ;
#23418=ORIENTED_EDGE ( 'NONE', *, *, #52187, .F. ) ;
#23421=VECTOR ( 'NONE', #23873, 1000.000000000000000 ) ;
#23426=DIRECTION ( 'NONE',  ( 0.3543493200069162685, -0.000000000000000000, -0.9351131265310288487 ) ) ;
#23427=VERTEX_POINT ( 'NONE', #37877 ) ;
#23428=CARTESIAN_POINT ( 'NONE',  ( 34.49999999999976552, 7.464255608400424791, 4.994342998332163219 ) ) ;
#23429=FACE_OUTER_BOUND ( 'NONE', #130491, .T. ) ;
#23430=VECTOR ( 'NONE', #23889, 1000.000000000000000 ) ;
#23431=AXIS2_PLACEMENT_3D ( 'NONE', #26413, #40170, #93091 ) ;
#23432=VECTOR ( 'NONE', #45735, 999.9999999999998863 ) ;
#23433=VECTOR ( 'NONE', #71301, 1000.000000000000000 ) ;
#23434=CARTESIAN_POINT ( 'NONE',  ( 30.70710678118632941, -9.740707523384177335, 5.000000000000000000 ) ) ;
#23435=ADVANCED_FACE ( 'NONE', ( #49482 ), #38568, .F. ) ;
#23436=FACE_BOUND ( 'NONE', #81848, .T. ) ;
#23437=LINE ( 'NONE', #122753, #38657 ) ;
#23438=ADVANCED_FACE ( 'NONE', ( #133089 ), #96473, .F. ) ;
#23439=DIRECTION ( 'NONE',  ( 0.7071067811865486830, -0.7071067811865464625, -0.000000000000000000 ) ) ;
#23440=VECTOR ( 'NONE', #127914, 1000.000000000000000 ) ;
#23442=LINE ( 'NONE', #90875, #85222 ) ;
#23443=ORIENTED_EDGE ( 'NONE', *, *, #133759, .T. ) ;
#23444=DIRECTION ( 'NONE',  ( 0.7071067811865487940, -0.7071067811865463515, 0.000000000000000000 ) ) ;
#23445=VERTEX_POINT ( 'NONE', #83516 ) ;
#23447=ORIENTED_EDGE ( 'NONE', *, *, #121990, .T. ) ;
#23450=LINE ( 'NONE', #44541, #12902 ) ;
#23451=AXIS2_PLACEMENT_3D ( 'NONE', #59488, #136298, #94216 ) ;
#23452=DIRECTION ( 'NONE',  ( 0.000000000000000000, 0.000000000000000000, -1.000000000000000000 ) ) ;
#23454=DIRECTION ( 'NONE',  ( 0.7071067811865487940, -0.7071067811865463515, 0.000000000000000000 ) ) ;
#23455=ADVANCED_FACE ( 'NONE', ( #29813 ), #127732, .F. ) ;
#23459=EDGE_CURVE ( 'NONE', #132715, #98945, #18198, .T. ) ;
#23460=FACE_OUTER_BOUND ( 'NONE', #4259, .T. ) ;
#23461=CARTESIAN_POINT ( 'NONE',  ( -34.42500000000000426, 10.54139925780190801, 5.000000000000000000 ) ) ;
#23462=LINE ( 'NONE', #66986, #101380 ) ;
#23463=DIRECTION ( 'NONE',  ( -0.7071067811865487940, 0.7071067811865463515, -0.000000000000000000 ) ) ;
#23464=VECTOR ( 'NONE', #73423, 1000.000000000000000 ) ;
#23466=DIRECTION ( 'NONE',  ( 0.6830127018922180770, -0.6830127018922204085, -0.2588190451025213501 ) ) ;
#23467=VERTEX_POINT ( 'NONE', #8050 ) ;
#23468=EDGE_LOOP ( 'NONE', ( #135492, #32814, #95797, #17863 ) ) ;
#23469=AXIS2_PLACEMENT_3D ( 'NONE', #143367, #22981, #111451 ) ;
#23470=DIRECTION ( 'NONE',  ( 0.000000000000000000, 0.000000000000000000, -1.000000000000000000 ) ) ;
#23472=ORIENTED_EDGE ( 'NONE', *, *, #101844, .T. ) ;
#23473=ORIENTED_EDGE ( 'NONE', *, *, #10903, .T. ) ;
#23474=ORIENTED_EDGE ( 'NONE', *, *, #66907, .F. ) ;
#23475=VECTOR ( 'NONE', #10158, 1000.000000000000000 ) ;
#23476=EDGE_CURVE ( 'NONE', #24896, #64028, #84244, .T. ) ;
#23479=VERTEX_POINT ( 'NONE', #74793 ) ;
#23480=LINE ( 'NONE', #2415, #23174 ) ;
#23484=ORIENTED_EDGE ( 'NONE', *, *, #24859, .F. ) ;
#23486=CARTESIAN_POINT ( 'NONE',  ( -17.39060256275758221, -2.561874075326514788, 4.636692559446314199 ) ) ;
#23487=VECTOR ( 'NONE', #22484, 1000.000000000000000 ) ;
#23488=CARTESIAN_POINT ( 'NONE',  ( -71.99451991528749772, 28.92564299267988304, 4.000000000000000000 ) ) ;
#23489=PLANE ( 'NONE',  #109654 ) ;
#23491=AXIS2_PLACEMENT_3D ( 'NONE', #121576, #67218, #502 ) ;
#23492=VERTEX_POINT ( 'NONE', #52285 ) ;
#23494=LINE ( 'NONE', #123564, #7470 ) ;
#23495=DIRECTION ( 'NONE',  ( -0.000000000000000000, 0.000000000000000000, 1.000000000000000000 ) ) ;
#23496=EDGE_LOOP ( 'NONE', ( #46636, #8377, #22534, #85133, #58555 ) ) ;
#23498=ORIENTED_EDGE ( 'NONE', *, *, #86853, .F. ) ;
#23499=VECTOR ( 'NONE', #38044, 1000.000000000000000 ) ;
#23501=CARTESIAN_POINT ( 'NONE',  ( 6.938893903907228378E-15, -22.06887692260758627, 4.000000000000000000 ) ) ;
#23502=CARTESIAN_POINT ( 'NONE',  ( -3.489213562373097322, -27.52281430457057709, 5.000000000000000000 ) ) ;
#23503=VECTOR ( 'NONE', #106574, 1000.000000000000000 ) ;
#23504=CARTESIAN_POINT ( 'NONE',  ( -34.42500000000001137, -0.02281430457058350458, 5.000000000000000000 ) ) ;
#23505=DIRECTION ( 'NONE',  ( -0.7071067811865487940, 0.7071067811865463515, -0.000000000000000000 ) ) ;
#23506=DIRECTION ( 'NONE',  ( -0.3543493200069162685, -0.000000000000000000, -0.9351131265310288487 ) ) ;
#23508=CARTESIAN_POINT ( 'NONE',  ( -34.92500000000001137, 22.22500000000000142, 4.000000000000000000 ) ) ;
#23509=DIRECTION ( 'NONE',  ( -0.7071067811865487940, -0.7071067811865463515, -0.000000000000000000 ) ) ;
#23510=VERTEX_POINT ( 'NONE', #51600 ) ;
#23511=EDGE_LOOP ( 'NONE', ( #5596, #45703, #41920, #84206 ) ) ;
#23513=CARTESIAN_POINT ( 'NONE',  ( -0.3281693992235289459, 14.25929247661557042, 4.000000000000000000 ) ) ;
#23514=( BOUNDED_CURVE ( )  B_SPLINE_CURVE ( 3, ( #103990, #140234, #38773, #30017 ),
 .UNSPECIFIED., .F., .T. ) 
 B_SPLINE_CURVE_WITH_KNOTS ( ( 4, 4 ),
 ( 4.350170835173025274, 4.500739107949256912 ),
 .UNSPECIFIED. ) 
 CURVE ( )  GEOMETRIC_REPRESENTATION_ITEM ( )  RATIONAL_B_SPLINE_CURVE ( ( 1.000000000000000000, 0.9981116584018945304, 0.9981116584018945304, 1.000000000000000000 ) ) 
 REPRESENTATION_ITEM ( '' )  );
#23515=CYLINDRICAL_SURFACE ( 'NONE', #25025, 0.5000000000000004441 ) ;
#23517=VERTEX_POINT ( 'NONE', #18949 ) ;
#23519=CARTESIAN_POINT ( 'NONE',  ( -15.48921356237309510, -27.52281430457066236, 5.000000000000000000 ) ) ;
#23520=LINE ( 'NONE', #13342, #139371 ) ;
#23521=EDGE_CURVE ( 'NONE', #16006, #84048, #63211, .T. ) ;
#23522=ORIENTED_EDGE ( 'NONE', *, *, #54209, .T. ) ;
#23524=LINE ( 'NONE', #22086, #7154 ) ;
#23525=EDGE_CURVE ( 'NONE', #72338, #128631, #86368, .T. ) ;
#23527=AXIS2_PLACEMENT_3D ( 'NONE', #1199, #111400, #102695 ) ;
#23528=CARTESIAN_POINT ( 'NONE',  ( 29.29289321881324781, 17.25929247661554200, 5.000000000000000000 ) ) ;
#23529=EDGE_CURVE ( 'NONE', #110079, #445, #8732, .T. ) ;
#23531=CARTESIAN_POINT ( 'NONE',  ( 26.99999999999980815, -8.151047557385048492, -8.977947279169864458 ) ) ;
#23532=AXIS2_PLACEMENT_3D ( 'NONE', #27174, #40236, #103997 ) ;
#23533=LINE ( 'NONE', #77245, #127491 ) ;
#23534=DIRECTION ( 'NONE',  ( -0.7071067811865486830, 0.7071067811865464625, 0.000000000000000000 ) ) ;
#23535=ORIENTED_EDGE ( 'NONE', *, *, #108964, .T. ) ;
#23536=EDGE_CURVE ( 'NONE', #90132, #111726, #119656, .T. ) ;
#23540=VECTOR ( 'NONE', #99129, 1000.000000000000000 ) ;
#23541=CARTESIAN_POINT ( 'NONE',  ( 7.499999999999949374, 12.05218569542904561, 5.000000000000000000 ) ) ;
#23542=VECTOR ( 'NONE', #120765, 1000.000000000000000 ) ;
#23544=CARTESIAN_POINT ( 'NONE',  ( -12.18398860626900060, 28.73617430169795739, 5.000000000000000000 ) ) ;
#23545=DIRECTION ( 'NONE',  ( -0.3543493200069162685, -0.000000000000000000, -0.9351131265310288487 ) ) ;
#23546=EDGE_CURVE ( 'NONE', #80500, #123836, #138604, .T. ) ;
#23547=CARTESIAN_POINT ( 'NONE',  ( -35.99451991528749772, 28.92564299267963079, 4.000000000000000000 ) ) ;
#23550=CYLINDRICAL_SURFACE ( 'NONE', #126409, 0.5000000000000004441 ) ;
#23551=EDGE_LOOP ( 'NONE', ( #80888, #27220, #41014, #78092 ) ) ;
#23552=ORIENTED_EDGE ( 'NONE', *, *, #117463, .T. ) ;
#23553=DIRECTION ( 'NONE',  ( -0.000000000000000000, -0.3543493200069152693, 0.9351131265310292928 ) ) ;
#23554=DIRECTION ( 'NONE',  ( -0.6830127018922181881, 0.6830127018922202975, -0.2588190451025214056 ) ) ;
#23555=CARTESIAN_POINT ( 'NONE',  ( 0.000000000000000000, 0.000000000000000000, 5.000000000000000000 ) ) ;
#23556=EDGE_CURVE ( 'NONE', #23783, #77634, #55160, .T. ) ;
#23559=CARTESIAN_POINT ( 'NONE',  ( 17.50183651486032943, -17.24070752338410628, 8.407044977365183414 ) ) ;
#23561=ORIENTED_EDGE ( 'NONE', *, *, #140594, .T. ) ;
#23564=CARTESIAN_POINT ( 'NONE',  ( -66.48921356237309510, -27.52281430457101763, 5.000000000000000000 ) ) ;
#23565=CARTESIAN_POINT ( 'NONE',  ( -6.183988606268994381, 28.73617430169791476, 5.000000000000000000 ) ) ;
#23566=EDGE_CURVE ( 'NONE', #28263, #142286, #44297, .T. ) ;
#23568=AXIS2_PLACEMENT_3D ( 'NONE', #141883, #67914, #14185 ) ;
#23569=DIRECTION ( 'NONE',  ( 0.7071067811865487940, -0.7071067811865463515, 0.000000000000000000 ) ) ;
#23572=AXIS2_PLACEMENT_3D ( 'NONE', #84148, #51499, #19560 ) ;
#23574=ORIENTED_EDGE ( 'NONE', *, *, #89215, .F. ) ;
#23575=ORIENTED_EDGE ( 'NONE', *, *, #132041, .F. ) ;
#23576=VECTOR ( 'NONE', #29103, 1000.000000000000000 ) ;
#23577=CARTESIAN_POINT ( 'NONE',  ( -23.29289321881329755, -6.740707523384218192, 5.000000000000000000 ) ) ;
#23578=DIRECTION ( 'NONE',  ( -0.7071067811865487940, 0.7071067811865463515, 0.000000000000000000 ) ) ;
#23579=CARTESIAN_POINT ( 'NONE',  ( 12.18398860626900060, 28.73617430169795739, 5.000000000000000000 ) ) ;
#23580=FACE_OUTER_BOUND ( 'NONE', #121217, .T. ) ;
#23581=LINE ( 'NONE', #1780, #68489 ) ;
#23582=EDGE_LOOP ( 'NONE', ( #107551, #79467, #82377, #38533 ) ) ;
#23583=DIRECTION ( 'NONE',  ( -0.7071067811865487940, 0.7071067811865463515, -0.000000000000000000 ) ) ;
#23584=CARTESIAN_POINT ( 'NONE',  ( -0.005480084712502889671, 28.92564299267938210, 4.000000000000000000 ) ) ;
#23585=LINE ( 'NONE', #133098, #70342 ) ;
#23587=DIRECTION ( 'NONE',  ( 0.7071067811865486830, -0.7071067811865464625, -0.000000000000000000 ) ) ;
#23588=ORIENTED_EDGE ( 'NONE', *, *, #25508, .F. ) ;
#23589=EDGE_CURVE ( 'NONE', #14142, #71472, #110217, .T. ) ;
#23590=VERTEX_POINT ( 'NONE', #76197 ) ;
#23592=ORIENTED_EDGE ( 'NONE', *, *, #11709, .F. ) ;
#23594=DIRECTION ( 'NONE',  ( 0.7071067811865486830, -0.7071067811865464625, -0.000000000000000000 ) ) ;
#23595=LINE ( 'NONE', #77307, #54881 ) ;
#23597=VECTOR ( 'NONE', #94711, 999.9999999999998863 ) ;
#23599=CARTESIAN_POINT ( 'NONE',  ( 5.816011393731002066, 28.73617430169783304, 5.000000000000000000 ) ) ;
#23600=VERTEX_POINT ( 'NONE', #12344 ) ;
#23602=VECTOR ( 'NONE', #119784, 1000.000000000000000 ) ;
#23605=ORIENTED_EDGE ( 'NONE', *, *, #141115, .F. ) ;
#23606=EDGE_CURVE ( 'NONE', #138104, #121, #142182, .T. ) ;
#23607=FACE_OUTER_BOUND ( 'NONE', #133321, .T. ) ;
#23608=CARTESIAN_POINT ( 'NONE',  ( -24.79289321881328334, 12.75929247661558463, 5.000000000000000000 ) ) ;
#23609=VECTOR ( 'NONE', #139448, 1000.000000000000000 ) ;
#23610=ORIENTED_EDGE ( 'NONE', *, *, #28044, .F. ) ;
#23611=EDGE_CURVE ( 'NONE', #87888, #64475, #56632, .T. ) ;
#23612=FACE_BOUND ( 'NONE', #73677, .T. ) ;
#23613=DIRECTION ( 'NONE',  ( 0.7071067811865487940, 0.7071067811865463515, 0.000000000000000000 ) ) ;
#23614=PLANE ( 'NONE',  #79144 ) ;
#23615=DIRECTION ( 'NONE',  ( 0.7071067811865487940, -0.7071067811865463515, 0.000000000000000000 ) ) ;
#23616=VECTOR ( 'NONE', #78133, 999.9999999999998863 ) ;
#23617=DIRECTION ( 'NONE',  ( 0.7071067811865487940, 0.7071067811865463515, 0.000000000000000000 ) ) ;
#23618=LINE ( 'NONE', #132432, #136903 ) ;
#23620=ORIENTED_EDGE ( 'NONE', *, *, #49553, .F. ) ;
#23621=ORIENTED_EDGE ( 'NONE', *, *, #56613, .T. ) ;
#23623=VERTEX_POINT ( 'NONE', #108775 ) ;
#23624=CARTESIAN_POINT ( 'NONE',  ( 69.29974487139159578, -27.71228299555254537, 4.000000000000000000 ) ) ;
#23625=EDGE_LOOP ( 'NONE', ( #83972, #64722, #84187, #82173 ) ) ;
#23626=DIRECTION ( 'NONE',  ( -0.000000000000000000, -0.3543493200069152693, 0.9351131265310292928 ) ) ;
#23627=VECTOR ( 'NONE', #59063, 999.9999999999998863 ) ;
#23629=AXIS2_PLACEMENT_3D ( 'NONE', #86198, #120949, #130426 ) ;
#23631=VECTOR ( 'NONE', #54198, 1000.000000000000000 ) ;
#23633=FACE_OUTER_BOUND ( 'NONE', #48634, .T. ) ;
#23634=ORIENTED_EDGE ( 'NONE', *, *, #72112, .F. ) ;
#23635=CARTESIAN_POINT ( 'NONE',  ( -25.08567745463940213, 22.22500000000000142, 8.728487125628603849 ) ) ;
#23636=LINE ( 'NONE', #44731, #5591 ) ;
#23637=EDGE_CURVE ( 'NONE', #6676, #45046, #31970, .T. ) ;
#23638=DIRECTION ( 'NONE',  ( -0.000000000000000000, -0.3543493200069152693, 0.9351131265310292928 ) ) ;
#23639=DIRECTION ( 'NONE',  ( 0.7071067811865487940, 0.7071067811865463515, 0.000000000000000000 ) ) ;
#23640=DIRECTION ( 'NONE',  ( 0.7071067811865486830, -0.7071067811865464625, -0.000000000000000000 ) ) ;
#23641=CARTESIAN_POINT ( 'NONE',  ( -10.49999999999992895, 14.14708470758590408, -0.5283514160166316032 ) ) ;
#23642=DIRECTION ( 'NONE',  ( 0.6830127018922181881, 0.6830127018922202975, -0.2588190451025214056 ) ) ;
#23643=AXIS2_PLACEMENT_3D ( 'NONE', #128597, #83695, #65520 ) ;
#23644=AXIS2_PLACEMENT_3D ( 'NONE', #106247, #40343, #87400 ) ;
#23645=AXIS2_PLACEMENT_3D ( 'NONE', #129326, #52484, #117711 ) ;
#23647=ORIENTED_EDGE ( 'NONE', *, *, #113987, .T. ) ;
#23648=LINE ( 'NONE', #133151, #123650 ) ;
#23649=CARTESIAN_POINT ( 'NONE',  ( 66.18398860626901126, 28.73617430169833753, 5.000000000000000000 ) ) ;
#23650=ORIENTED_EDGE ( 'NONE', *, *, #133980, .T. ) ;
#23651=EDGE_CURVE ( 'NONE', #49245, #69087, #87780, .T. ) ;
#23652=VERTEX_POINT ( 'NONE', #122532 ) ;
#23653=EDGE_CURVE ( 'NONE', #134939, #126282, #79083, .T. ) ;
#23654=ORIENTED_EDGE ( 'NONE', *, *, #135523, .F. ) ;
#23656=ORIENTED_EDGE ( 'NONE', *, *, #88915, .T. ) ;
#23657=CARTESIAN_POINT ( 'NONE',  ( -32.99999999999976552, -1.447814304570818500, 5.000000000000000000 ) ) ;
#23660=EDGE_LOOP ( 'NONE', ( #71624, #140277, #117546, #22585 ) ) ;
#23664=ORIENTED_EDGE ( 'NONE', *, *, #109523, .T. ) ;
#23665=ADVANCED_FACE ( 'NONE', ( #65348 ), #76937, .F. ) ;
#23666=DIRECTION ( 'NONE',  ( -0.7071067811865486830, -0.7071067811865464625, -0.000000000000000000 ) ) ;
#23669=DIRECTION ( 'NONE',  ( 0.6830127018922181881, 0.6830127018922202975, -0.2588190451025214056 ) ) ;
#23670=VERTEX_POINT ( 'NONE', #54466 ) ;
#23671=VECTOR ( 'NONE', #27001, 1000.000000000000000 ) ;
#23672=DIRECTION ( 'NONE',  ( 0.7071067811865487940, -0.7071067811865463515, 0.000000000000000000 ) ) ;
#23673=ORIENTED_EDGE ( 'NONE', *, *, #5775, .F. ) ;
#23674=VECTOR ( 'NONE', #123898, 1000.000000000000000 ) ;
#23675=ORIENTED_EDGE ( 'NONE', *, *, #143448, .T. ) ;
#23677=DIRECTION ( 'NONE',  ( 0.6830127018922181881, 0.6830127018922202975, -0.2588190451025214056 ) ) ;
#23678=VECTOR ( 'NONE', #120927, 1000.000000000000000 ) ;
#23679=PLANE ( 'NONE',  #97769 ) ;
#23680=DIRECTION ( 'NONE',  ( -0.6830127018922180770, -0.6830127018922204085, -0.2588190451025213501 ) ) ;
#23682=CARTESIAN_POINT ( 'NONE',  ( -1.171830600776468945, 18.75929247661553134, 4.000000000000000000 ) ) ;
#23683=ORIENTED_EDGE ( 'NONE', *, *, #58939, .T. ) ;
#23684=VECTOR ( 'NONE', #22541, 999.9999999999998863 ) ;
#23685=CARTESIAN_POINT ( 'NONE',  ( 54.18398860626899705, 28.73617430169825226, 5.000000000000000000 ) ) ;
#23687=DIRECTION ( 'NONE',  ( -0.3543493200069162685, -0.000000000000000000, -0.9351131265310288487 ) ) ;
#23688=EDGE_CURVE ( 'NONE', #115745, #4418, #43559, .T. ) ;
#23689=CARTESIAN_POINT ( 'NONE',  ( 0.000000000000000000, 0.000000000000000000, 5.000000000000000000 ) ) ;
#23690=CARTESIAN_POINT ( 'NONE',  ( -6.183988606268994381, 28.73617430169791476, 5.000000000000000000 ) ) ;
#23691=ORIENTED_EDGE ( 'NONE', *, *, #137850, .T. ) ;
#23693=ORIENTED_EDGE ( 'NONE', *, *, #98453, .T. ) ;
#23694=AXIS2_PLACEMENT_3D ( 'NONE', #109899, #54825, #122924 ) ;
#23697=CARTESIAN_POINT ( 'NONE',  ( -20.99999999999985079, -4.068876922607771895, 4.000000000000000000 ) ) ;
#23698=DIRECTION ( 'NONE',  ( -0.6830127018922181881, 0.6830127018922202975, -0.2588190451025214056 ) ) ;
#23699=DIRECTION ( 'NONE',  ( 0.6830127018922181881, 0.6830127018922202975, -0.2588190451025214056 ) ) ;
#23700=EDGE_CURVE ( 'NONE', #127570, #19214, #100090, .T. ) ;
#23702=EDGE_CURVE ( 'NONE', #83048, #122228, #23199, .T. ) ;
#23703=CARTESIAN_POINT ( 'NONE',  ( 60.18398860626900415, 28.73617430169829490, 5.000000000000000000 ) ) ;
#23704=LINE ( 'NONE', #46210, #52545 ) ;
#23705=DIRECTION ( 'NONE',  ( 0.7071067811865487940, 0.7071067811865463515, 0.000000000000000000 ) ) ;
#23706=DIRECTION ( 'NONE',  ( -0.7071067811865486830, -0.7071067811865464625, 0.000000000000000000 ) ) ;
#23707=ORIENTED_EDGE ( 'NONE', *, *, #94300, .F. ) ;
#23708=PLANE ( 'NONE',  #76584 ) ;
#23709=AXIS2_PLACEMENT_3D ( 'NONE', #68152, #22422, #55092 ) ;
#23710=ORIENTED_EDGE ( 'NONE', *, *, #92408, .F. ) ;
#23713=DIRECTION ( 'NONE',  ( -0.6830127018922181881, 0.6830127018922202975, -0.2588190451025214056 ) ) ;
#23714=LINE ( 'NONE', #67985, #27892 ) ;
#23715=ORIENTED_EDGE ( 'NONE', *, *, #41148, .T. ) ;
#23716=EDGE_CURVE ( 'NONE', #13610, #136798, #111678, .T. ) ;
#23717=EDGE_CURVE ( 'NONE', #35748, #50158, #69625, .T. ) ;
#23718=PLANE ( 'NONE',  #132910 ) ;
#23719=VERTEX_POINT ( 'NONE', #71043 ) ;
#23720=DIRECTION ( 'NONE',  ( -0.7071067811865487940, 0.7071067811865463515, 0.000000000000000000 ) ) ;
#23722=ORIENTED_EDGE ( 'NONE', *, *, #30900, .F. ) ;
#23723=DIRECTION ( 'NONE',  ( 0.000000000000000000, 1.000000000000000000, 0.000000000000000000 ) ) ;
#23724=ORIENTED_EDGE ( 'NONE', *, *, #51989, .F. ) ;
#23725=DIRECTION ( 'NONE',  ( -0.7071067811865487940, 0.7071067811865463515, -0.000000000000000000 ) ) ;
#23726=EDGE_CURVE ( 'NONE', #47652, #130156, #81203, .T. ) ;
#23730=ORIENTED_EDGE ( 'NONE', *, *, #132629, .T. ) ;
#23731=CARTESIAN_POINT ( 'NONE',  ( -10.17183060077639745, -14.24070752338413648, 4.000000000000000000 ) ) ;
#23732=CARTESIAN_POINT ( 'NONE',  ( 26.18753812416034421, -22.22500000000000142, 4.000000000000000000 ) ) ;
#23733=DIRECTION ( 'NONE',  ( 0.7071067811865486830, -0.7071067811865464625, -0.000000000000000000 ) ) ;
#23737=EDGE_CURVE ( 'NONE', #28591, #136607, #15873, .T. ) ;
#23739=VECTOR ( 'NONE', #20564, 1000.000000000000000 ) ;
#23740=DIRECTION ( 'NONE',  ( 0.6830127018922180770, -0.6830127018922204085, -0.2588190451025213501 ) ) ;
#23742=ORIENTED_EDGE ( 'NONE', *, *, #63225, .F. ) ;
#23743=( BOUNDED_CURVE ( )  B_SPLINE_CURVE ( 3, ( #73854, #27470, #39831, #18729 ),
 .UNSPECIFIED., .F., .F. ) 
 B_SPLINE_CURVE_WITH_KNOTS ( ( 4, 4 ),
 ( 5.143245962375958769, 6.645403452391247079 ),
 .UNSPECIFIED. ) 
 CURVE ( )  GEOMETRIC_REPRESENTATION_ITEM ( )  RATIONAL_B_SPLINE_CURVE ( ( 1.000000000000000000, 0.8206354192515226131, 0.8206354192515226131, 1.000000000000000000 ) ) 
 REPRESENTATION_ITEM ( '' )  );
#23745=VECTOR ( 'NONE', #3838, 1000.000000000000000 ) ;
#23746=LINE ( 'NONE', #68013, #72333 ) ;
#23749=LINE ( 'NONE', #89711, #61629 ) ;
#23750=LINE ( 'NONE', #2688, #115730 ) ;
#23752=EDGE_CURVE ( 'NONE', #97758, #116142, #38397, .T. ) ;
#23753=LINE ( 'NONE', #68020, #7579 ) ;
#23755=COLOUR_RGB ( '', 0.31764706, 0.68627451, 0.89019608) ;
#23756=CARTESIAN_POINT ( 'NONE',  ( 32.99999999999977973, 20.96639925780204905, 5.000000000000000000 ) ) ;
#23757=EDGE_LOOP ( 'NONE', ( #112666, #125837, #18940, #79920 ) ) ;
#23758=CARTESIAN_POINT ( 'NONE',  ( -12.29974487139158512, -27.71228299555214747, 4.000000000000000000 ) ) ;
#23759=PLANE ( 'NONE',  #115983 ) ;
#23760=CARTESIAN_POINT ( 'NONE',  ( -17.27718569542927796, -21.72500000000000142, 5.000000000000000000 ) ) ;
#23761=ORIENTED_EDGE ( 'NONE', *, *, #117550, .F. ) ;
#23762=CARTESIAN_POINT ( 'NONE',  ( -69.48921356237309510, -27.52281430457103895, 5.000000000000000000 ) ) ;
#23763=DIRECTION ( 'NONE',  ( -0.000000000000000000, 0.3543493200069153248, 0.9351131265310292928 ) ) ;
#23764=EDGE_CURVE ( 'NONE', #97802, #118711, #57322, .T. ) ;
#23765=VERTEX_POINT ( 'NONE', #113809 ) ;
#23767=ADVANCED_FACE ( 'NONE', ( #4999 ), #25362, .T. ) ;
#23769=DIRECTION ( 'NONE',  ( -0.7071067811865486830, -0.7071067811865464625, 0.000000000000000000 ) ) ;
#23770=CARTESIAN_POINT ( 'NONE',  ( -54.18398860626899705, 28.73617430169825226, 5.000000000000000000 ) ) ;
#23771=LINE ( 'NONE', #10711, #23678 ) ;
#23772=ORIENTED_EDGE ( 'NONE', *, *, #107140, .F. ) ;
#23777=VECTOR ( 'NONE', #2463, 999.9999999999998863 ) ;
#23778=ORIENTED_EDGE ( 'NONE', *, *, #9826, .F. ) ;
#23779=CARTESIAN_POINT ( 'NONE',  ( -3.707106781186512823, -9.740707523384184441, 5.000000000000000000 ) ) ;
#23781=CARTESIAN_POINT ( 'NONE',  ( 26.99999999999981171, 2.342191155542478587, -5.001666872980147893 ) ) ;
#23782=DIRECTION ( 'NONE',  ( -0.6830127018922181881, 0.6830127018922202975, -0.2588190451025214056 ) ) ;
#23783=VERTEX_POINT ( 'NONE', #90653 ) ;
#23785=DIRECTION ( 'NONE',  ( -0.6830127018922180770, -0.6830127018922204085, -0.2588190451025213501 ) ) ;
#23787=CARTESIAN_POINT ( 'NONE',  ( -17.16347128873440298, 15.75929247661555799, 9.299976744542879814 ) ) ;
#23789=ORIENTED_EDGE ( 'NONE', *, *, #55586, .T. ) ;
#23791=CARTESIAN_POINT ( 'NONE',  ( 42.29974487139158157, -27.71228299555235708, 4.000000000000000000 ) ) ;
#23792=CARTESIAN_POINT ( 'NONE',  ( -12.48921356237309155, -27.52281430457064104, 5.000000000000000000 ) ) ;
#23793=AXIS2_PLACEMENT_3D ( 'NONE', #62645, #32143, #98811 ) ;
#23794=ORIENTED_EDGE ( 'NONE', *, *, #10112, .F. ) ;
#23796=DIRECTION ( 'NONE',  ( -0.000000000000000000, 0.000000000000000000, 1.000000000000000000 ) ) ;
#23797=CARTESIAN_POINT ( 'NONE',  ( -20.99999999999984368, -4.447814304570784749, 5.000000000000000000 ) ) ;
#23799=LINE ( 'NONE', #1987, #104449 ) ;
#23800=LINE ( 'NONE', #113646, #89578 ) ;
#23801=CARTESIAN_POINT ( 'NONE',  ( 4.499999999999965361, 15.43112307739203182, 4.000000000000000000 ) ) ;
#23802=CARTESIAN_POINT ( 'NONE',  ( -34.82816939922327748, 15.75929247661556332, 4.000000000000000000 ) ) ;
#23804=ORIENTED_EDGE ( 'NONE', *, *, #137652, .F. ) ;
#23805=ORIENTED_EDGE ( 'NONE', *, *, #73933, .T. ) ;
#23807=VERTEX_POINT ( 'NONE', #91373 ) ;
#23808=ADVANCED_FACE ( 'NONE', ( #47190 ), #35582, .F. ) ;
#23809=ORIENTED_EDGE ( 'NONE', *, *, #14061, .F. ) ;
#23810=AXIS2_PLACEMENT_3D ( 'NONE', #49514, #15375, #61799 ) ;
#23811=AXIS2_PLACEMENT_3D ( 'NONE', #130928, #18531, #141049 ) ;
#23812=FACE_OUTER_BOUND ( 'NONE', #122641, .T. ) ;
#23813=ORIENTED_EDGE ( 'NONE', *, *, #77932, .T. ) ;
#23814=PLANE ( 'NONE',  #11197 ) ;
#23815=LINE ( 'NONE', #14360, #47192 ) ;
#23817=DIRECTION ( 'NONE',  ( -0.7071067811865487940, 0.7071067811865463515, -0.000000000000000000 ) ) ;
#23818=VECTOR ( 'NONE', #116503, 1000.000000000000000 ) ;
#23819=CARTESIAN_POINT ( 'NONE',  ( -15.48921356237309510, -27.52281430457066236, 5.000000000000000000 ) ) ;
#23820=ORIENTED_EDGE ( 'NONE', *, *, #20725, .T. ) ;
#23821=DIRECTION ( 'NONE',  ( 0.7071067811865486830, -0.7071067811865464625, -0.000000000000000000 ) ) ;
#23822=ORIENTED_EDGE ( 'NONE', *, *, #97081, .F. ) ;
#23823=ADVANCED_FACE ( 'NONE', ( #134886 ), #126125, .F. ) ;
#23824=DIRECTION ( 'NONE',  ( 0.000000000000000000, 0.000000000000000000, -1.000000000000000000 ) ) ;
#23826=DIRECTION ( 'NONE',  ( -0.000000000000000000, 0.000000000000000000, 1.000000000000000000 ) ) ;
#23827=ORIENTED_EDGE ( 'NONE', *, *, #11058, .T. ) ;
#23828=DIRECTION ( 'NONE',  ( 0.7071067811865486830, -0.7071067811865464625, -0.000000000000000000 ) ) ;
#23829=EDGE_CURVE ( 'NONE', #20167, #103522, #26799, .T. ) ;
#23833=VERTEX_POINT ( 'NONE', #93488 ) ;
#23836=DIRECTION ( 'NONE',  ( 0.7071067811865487940, 0.7071067811865463515, 0.000000000000000000 ) ) ;
#23838=DIRECTION ( 'NONE',  ( 0.3543493200069162685, -0.000000000000000000, -0.9351131265310288487 ) ) ;
#23839=EDGE_CURVE ( 'NONE', #98820, #106359, #102944, .T. ) ;
#23840=DIRECTION ( 'NONE',  ( 0.7071067811865486830, -0.7071067811865464625, -0.000000000000000000 ) ) ;
#23841=PLANE ( 'NONE',  #29684 ) ;
#23843=DIRECTION ( 'NONE',  ( -0.6830127018922181881, 0.6830127018922202975, -0.2588190451025214056 ) ) ;
#23844=VECTOR ( 'NONE', #81304, 1000.000000000000227 ) ;
#23845=ADVANCED_FACE ( 'NONE', ( #126805 ), #68217, .T. ) ;
#23846=VECTOR ( 'NONE', #2771, 1000.000000000000227 ) ;
#23848=ORIENTED_EDGE ( 'NONE', *, *, #9039, .T. ) ;
#23849=CARTESIAN_POINT ( 'NONE',  ( -11.99999999999992006, 7.007997736742436423, -8.085015511992141413 ) ) ;
#23850=LINE ( 'NONE', #12942, #47629 ) ;
#23851=CARTESIAN_POINT ( 'NONE',  ( -30.29974487139158867, -27.71228299555227537, 4.000000000000000000 ) ) ;
#23852=ORIENTED_EDGE ( 'NONE', *, *, #38303, .F. ) ;
#23853=ORIENTED_EDGE ( 'NONE', *, *, #26376, .T. ) ;
#23854=VECTOR ( 'NONE', #107115, 1000.000000000000000 ) ;
#23857=ADVANCED_FACE ( 'NONE', ( #112394 ), #13753, .F. ) ;
#23858=ORIENTED_EDGE ( 'NONE', *, *, #9643, .F. ) ;
#23859=ORIENTED_EDGE ( 'NONE', *, *, #50507, .F. ) ;
#23860=CARTESIAN_POINT ( 'NONE',  ( -28.49999999999980815, -4.796895815301044586, -3.611700055028748579 ) ) ;
#23862=CARTESIAN_POINT ( 'NONE',  ( 0.000000000000000000, 0.000000000000000000, 5.000000000000000000 ) ) ;
#23863=DIRECTION ( 'NONE',  ( -0.7071067811865487940, 0.7071067811865463515, -0.000000000000000000 ) ) ;
#23864=ORIENTED_EDGE ( 'NONE', *, *, #59219, .T. ) ;
#23866=ORIENTED_EDGE ( 'NONE', *, *, #66290, .F. ) ;
#23867=LINE ( 'NONE', #68821, #12131 ) ;
#23868=VECTOR ( 'NONE', #40836, 999.9999999999998863 ) ;
#23870=ORIENTED_EDGE ( 'NONE', *, *, #109184, .T. ) ;
#23873=DIRECTION ( 'NONE',  ( -0.7071067811865486830, -0.7071067811865464625, 0.000000000000000000 ) ) ;
#23874=VERTEX_POINT ( 'NONE', #92043 ) ;
#23875=ADVANCED_FACE ( 'NONE', ( #36956 ), #26098, .F. ) ;
#23876=ORIENTED_EDGE ( 'NONE', *, *, #102805, .F. ) ;
#23878=CARTESIAN_POINT ( 'NONE',  ( 72.48921356237309510, -27.52281430457106026, 5.000000000000000000 ) ) ;
#23879=CARTESIAN_POINT ( 'NONE',  ( 0.000000000000000000, 0.000000000000000000, 5.000000000000000000 ) ) ;
#23880=CARTESIAN_POINT ( 'NONE',  ( -27.51665438641025574, 22.22500000000000142, 4.500000000000000888 ) ) ;
#23881=CARTESIAN_POINT ( 'NONE',  ( -42.18398860626899705, 28.73617430169816700, 5.000000000000000000 ) ) ;
#23882=DIRECTION ( 'NONE',  ( 0.7071067811865486830, -0.7071067811865464625, -0.000000000000000000 ) ) ;
#23884=VECTOR ( 'NONE', #55056, 1000.000000000000000 ) ;
#23885=EDGE_CURVE ( 'NONE', #121977, #27100, #27490, .T. ) ;
#23887=DIRECTION ( 'NONE',  ( 0.7071067811865487940, 0.7071067811865463515, 0.000000000000000000 ) ) ;
#23889=DIRECTION ( 'NONE',  ( 0.7071067811865487940, 0.7071067811865463515, -0.000000000000000000 ) ) ;
#23891=ORIENTED_EDGE ( 'NONE', *, *, #43145, .F. ) ;
#23893=DIRECTION ( 'NONE',  ( 0.7071067811865487940, -0.7071067811865463515, 0.000000000000000000 ) ) ;
#23894=ADVANCED_FACE ( 'NONE', ( #139149 ), #52117, .T. ) ;
#23896=VECTOR ( 'NONE', #112824, 1000.000000000000227 ) ;
#23898=ORIENTED_EDGE ( 'NONE', *, *, #107842, .T. ) ;
#23899=EDGE_CURVE ( 'NONE', #128651, #87872, #139871, .T. ) ;
#23900=ORIENTED_EDGE ( 'NONE', *, *, #35720, .T. ) ;
#23901=ADVANCED_FACE ( 'NONE', ( #96300 ), #72495, .F. ) ;
#23902=DIRECTION ( 'NONE',  ( -0.7071067811865486830, 0.7071067811865464625, 0.000000000000000000 ) ) ;
#23903=CARTESIAN_POINT ( 'NONE',  ( -1.499999999999989120, 18.05218569542898521, 5.000000000000000000 ) ) ;
#23904=VERTEX_POINT ( 'NONE', #128268 ) ;
#23905=CARTESIAN_POINT ( 'NONE',  ( 5.999999999999956479, 12.83542986846997813, -1.025386466790383810 ) ) ;
#23906=ORIENTED_EDGE ( 'NONE', *, *, #23829, .F. ) ;
#23907=VECTOR ( 'NONE', #113020, 1000.000000000000227 ) ;
#23908=CARTESIAN_POINT ( 'NONE',  ( -10.17183060077639389, -8.240707523384200428, 4.000000000000000000 ) ) ;
#23909=CARTESIAN_POINT ( 'NONE',  ( -63.18398860626900415, 28.73617430169831621, 5.000000000000000000 ) ) ;
#23910=DIRECTION ( 'NONE',  ( -0.7071067811865486830, 0.7071067811865464625, -0.000000000000000000 ) ) ;
#23911=VECTOR ( 'NONE', #66332, 1000.000000000000000 ) ;
#23912=ADVANCED_FACE ( 'NONE', ( #94885 ), #7879, .F. ) ;
#23914=FACE_OUTER_BOUND ( 'NONE', #6668, .T. ) ;
#23915=FACE_OUTER_BOUND ( 'NONE', #29153, .T. ) ;
#23916=CARTESIAN_POINT ( 'NONE',  ( 13.49999999999991473, 1.030536316426525989, -5.498701923753829490 ) ) ;
#23917=FACE_OUTER_BOUND ( 'NONE', #97376, .T. ) ;
#23920=VECTOR ( 'NONE', #35905, 1000.000000000000000 ) ;
#23921=PLANE ( 'NONE',  #6564 ) ;
#23922=EDGE_CURVE ( 'NONE', #29089, #2906, #86182, .T. ) ;
#23923=CARTESIAN_POINT ( 'NONE',  ( -14.29289321881335439, 17.25929247661554200, 5.000000000000000000 ) ) ;
#23924=PLANE ( 'NONE',  #75545 ) ;
#23925=VERTEX_POINT ( 'NONE', #39849 ) ;
#23926=EDGE_LOOP ( 'NONE', ( #347, #130375, #132994, #47429 ) ) ;
#23928=VERTEX_POINT ( 'NONE', #71756 ) ;
#23929=EDGE_LOOP ( 'NONE', ( #98168, #32572, #31518, #56574 ) ) ;
#23930=ORIENTED_EDGE ( 'NONE', *, *, #42551, .T. ) ;
#23932=DIRECTION ( 'NONE',  ( -0.3543493200069162685, -0.000000000000000000, -0.9351131265310288487 ) ) ;
#23933=VECTOR ( 'NONE', #25083, 1000.000000000000000 ) ;
#23934=PLANE ( 'NONE',  #75535 ) ;
#23935=VERTEX_POINT ( 'NONE', #62299 ) ;
#23936=FACE_OUTER_BOUND ( 'NONE', #85454, .T. ) ;
#23937=CARTESIAN_POINT ( 'NONE',  ( -30.79289321881324071, -14.24070752338413826, 5.000000000000000000 ) ) ;
#23938=CARTESIAN_POINT ( 'NONE',  ( -34.92500000000001137, 22.22500000000000142, 4.000000000000000000 ) ) ;
#23940=VERTEX_POINT ( 'NONE', #63027 ) ;
#23941=DIRECTION ( 'NONE',  ( 1.000000000000000000, 0.000000000000000000, 0.000000000000000000 ) ) ;
#23942=DIRECTION ( 'NONE',  ( -0.6830127018922181881, 0.6830127018922202975, -0.2588190451025214056 ) ) ;
#23943=DIRECTION ( 'NONE',  ( -0.6830127018922181881, 0.6830127018922202975, -0.2588190451025214056 ) ) ;
#23944=VECTOR ( 'NONE', #30918, 1000.000000000000000 ) ;
#23947=FACE_OUTER_BOUND ( 'NONE', #24959, .T. ) ;
#23949=DIRECTION ( 'NONE',  ( 0.6830127018922181881, 0.6830127018922202975, -0.2588190451025214056 ) ) ;
#23950=EDGE_CURVE ( 'NONE', #59256, #67860, #106459, .T. ) ;
#23951=EDGE_CURVE ( 'NONE', #16172, #104226, #127538, .T. ) ;
#23952=ORIENTED_EDGE ( 'NONE', *, *, #121994, .T. ) ;
#23953=ORIENTED_EDGE ( 'NONE', *, *, #115671, .F. ) ;
#23955=ORIENTED_EDGE ( 'NONE', *, *, #24429, .F. ) ;
#23956=DIRECTION ( 'NONE',  ( -0.7071067811865486830, 0.7071067811865464625, 0.000000000000000000 ) ) ;
#23957=VECTOR ( 'NONE', #39965, 1000.000000000000000 ) ;
#23958=DIRECTION ( 'NONE',  ( -0.7071067811865487940, 0.7071067811865463515, -0.000000000000000000 ) ) ;
#23960=PLANE ( 'NONE',  #125270 ) ;
#23964=VECTOR ( 'NONE', #128534, 1000.000000000000000 ) ;
#23965=DIRECTION ( 'NONE',  ( 0.7071067811865487940, 0.7071067811865463515, 0.000000000000000000 ) ) ;
#23967=ORIENTED_EDGE ( 'NONE', *, *, #79843, .F. ) ;
#23968=ORIENTED_EDGE ( 'NONE', *, *, #100533, .F. ) ;
#23969=CARTESIAN_POINT ( 'NONE',  ( -11.99999999999991651, -16.60178936734449806, 0.8616154019347220805 ) ) ;
#23974=ORIENTED_EDGE ( 'NONE', *, *, #2211, .T. ) ;
#23976=CARTESIAN_POINT ( 'NONE',  ( -24.18398860626899705, 28.73617430169804265, 5.000000000000000000 ) ) ;
#23978=VERTEX_POINT ( 'NONE', #28233 ) ;
#23979=ORIENTED_EDGE ( 'NONE', *, *, #80572, .F. ) ;
#23980=VECTOR ( 'NONE', #99606, 1000.000000000000000 ) ;
#23981=DIRECTION ( 'NONE',  ( -0.000000000000000000, -0.000000000000000000, 1.000000000000000000 ) ) ;
#23983=ORIENTED_EDGE ( 'NONE', *, *, #97510, .F. ) ;
#23984=AXIS2_PLACEMENT_3D ( 'NONE', #47902, #136297, #71074 ) ;
#23985=DIRECTION ( 'NONE',  ( -0.7071067811865486830, -0.7071067811865464625, -0.000000000000000000 ) ) ;
#23986=CARTESIAN_POINT ( 'NONE',  ( 36.18398860626899705, 28.73617430169812437, 5.000000000000000000 ) ) ;
#23988=VECTOR ( 'NONE', #57598, 1000.000000000000000 ) ;
#23989=EDGE_CURVE ( 'NONE', #4323, #86268, #51422, .T. ) ;
#23990=FACE_BOUND ( 'NONE', #86776, .T. ) ;
#23991=ORIENTED_EDGE ( 'NONE', *, *, #126923, .F. ) ;
#23993=EDGE_CURVE ( 'NONE', #128576, #36198, #118795, .T. ) ;
#23994=CARTESIAN_POINT ( 'NONE',  ( 0.000000000000000000, 0.000000000000000000, 5.000000000000000000 ) ) ;
#23996=CARTESIAN_POINT ( 'NONE',  ( 20.99451991528748707, 28.92564299267952777, 4.000000000000000000 ) ) ;
#23997=DIRECTION ( 'NONE',  ( -0.7071067811865487940, 0.7071067811865463515, -0.000000000000000000 ) ) ;
#23999=DIRECTION ( 'NONE',  ( -0.7071067811865486830, -0.7071067811865464625, 0.000000000000000000 ) ) ;
#24000=ORIENTED_EDGE ( 'NONE', *, *, #9486, .F. ) ;
#24001=ORIENTED_EDGE ( 'NONE', *, *, #94727, .F. ) ;
#24002=ORIENTED_EDGE ( 'NONE', *, *, #43553, .T. ) ;
#24004=EDGE_CURVE ( 'NONE', #81446, #19388, #41968, .T. ) ;
#24005=EDGE_CURVE ( 'NONE', #98543, #69474, #98478, .T. ) ;
#24008=ORIENTED_EDGE ( 'NONE', *, *, #51351, .F. ) ;
#24009=DIRECTION ( 'NONE',  ( 0.6830127018922180770, -0.6830127018922204085, -0.2588190451025213501 ) ) ;
#24010=CARTESIAN_POINT ( 'NONE',  ( -26.18650864602345507, -15.74070752338411694, 8.904080028139002678 ) ) ;
#24012=ORIENTED_EDGE ( 'NONE', *, *, #142972, .F. ) ;
#24013=CARTESIAN_POINT ( 'NONE',  ( -34.42500000000001137, -10.45860074219788416, 5.000000000000000000 ) ) ;
#24015=EDGE_CURVE ( 'NONE', #58244, #113958, #132578, .T. ) ;
#24017=DIRECTION ( 'NONE',  ( 0.7071067811865487940, 0.7071067811865463515, -0.000000000000000000 ) ) ;
#24019=CARTESIAN_POINT ( 'NONE',  ( 30.70710678118633652, -6.740707523384211086, 5.000000000000000000 ) ) ;
#24020=ORIENTED_EDGE ( 'NONE', *, *, #26078, .F. ) ;
#24021=ORIENTED_EDGE ( 'NONE', *, *, #124420, .T. ) ;
#24022=VECTOR ( 'NONE', #43838, 999.9999999999998863 ) ;
#24023=ORIENTED_EDGE ( 'NONE', *, *, #130808, .T. ) ;
#24024=VERTEX_POINT ( 'NONE', #54297 ) ;
#24025=DIRECTION ( 'NONE',  ( -0.7071067811865487940, 0.7071067811865463515, -0.000000000000000000 ) ) ;
#24026=ADVANCED_FACE ( 'NONE', ( #43395 ), #97762, .F. ) ;
#24027=EDGE_LOOP ( 'NONE', ( #80558, #123746, #94746, #141359 ) ) ;
#24028=ORIENTED_EDGE ( 'NONE', *, *, #22971, .T. ) ;
#24029=CARTESIAN_POINT ( 'NONE',  ( -30.47512612785027031, 14.25929247661557397, 9.797011795316567628 ) ) ;
#24030=DIRECTION ( 'NONE',  ( 1.000000000000000000, 0.000000000000000000, 0.000000000000000000 ) ) ;
#24031=VECTOR ( 'NONE', #138431, 999.9999999999998863 ) ;
#24032=ORIENTED_EDGE ( 'NONE', *, *, #57447, .F. ) ;
#24035=DIRECTION ( 'NONE',  ( -0.7071067811865487940, 0.7071067811865463515, 0.000000000000000000 ) ) ;
#24037=CARTESIAN_POINT ( 'NONE',  ( -27.48921356237309155, -27.52281430457074762, 5.000000000000000000 ) ) ;
#24038=ORIENTED_EDGE ( 'NONE', *, *, #76899, .F. ) ;
#24040=DIRECTION ( 'NONE',  ( -0.000000000000000000, 0.000000000000000000, 1.000000000000000000 ) ) ;
#24041=DIRECTION ( 'NONE',  ( -0.6830127018922181881, 0.6830127018922202975, -0.2588190451025214056 ) ) ;
#24042=LINE ( 'NONE', #90745, #97505 ) ;
#24043=ADVANCED_FACE ( 'NONE', ( #22310 ), #76759, .F. ) ;
#24044=ORIENTED_EDGE ( 'NONE', *, *, #65956, .F. ) ;
#24045=LINE ( 'NONE', #55249, #10215 ) ;
#24046=FACE_OUTER_BOUND ( 'NONE', #72030, .T. ) ;
#24047=EDGE_LOOP ( 'NONE', ( #137875, #80734, #38618, #42768 ) ) ;
#24048=DIRECTION ( 'NONE',  ( -0.000000000000000000, -0.3543493200069152693, 0.9351131265310292928 ) ) ;
#24049=VERTEX_POINT ( 'NONE', #143407 ) ;
#24050=PLANE ( 'NONE',  #128430 ) ;
#24051=CARTESIAN_POINT ( 'NONE',  ( -18.00548008471250583, 28.92564299267925776, 4.000000000000000000 ) ) ;
#24052=DIRECTION ( 'NONE',  ( 0.7071067811865486830, -0.7071067811865464625, -0.000000000000000000 ) ) ;
#24055=EDGE_CURVE ( 'NONE', #135397, #46535, #31099, .T. ) ;
#24057=EDGE_CURVE ( 'NONE', #102448, #93966, #45569, .T. ) ;
#24058=CARTESIAN_POINT ( 'NONE',  ( 26.99999999999981526, -16.60178936734445543, 0.8616154019348096771 ) ) ;
#24059=CARTESIAN_POINT ( 'NONE',  ( 1.499999999999997780, 10.08746187583914633, 4.000000000000000000 ) ) ;
#24060=EDGE_LOOP ( 'NONE', ( #76698, #78115, #20601, #70455 ) ) ;
#24061=CARTESIAN_POINT ( 'NONE',  ( -57.18398860626899705, 28.73617430169827358, 5.000000000000000000 ) ) ;
#24062=ADVANCED_FACE ( 'NONE', ( #20177 ), #21641, .T. ) ;
#24063=VERTEX_POINT ( 'NONE', #86900 ) ;
#24066=VERTEX_POINT ( 'NONE', #55711 ) ;
#24067=VERTEX_POINT ( 'NONE', #575 ) ;
#24069=CARTESIAN_POINT ( 'NONE',  ( -34.92500000000001137, 22.22500000000000142, 4.000000000000000000 ) ) ;
#24070=VECTOR ( 'NONE', #119898, 1000.000000000000000 ) ;
#24071=ORIENTED_EDGE ( 'NONE', *, *, #57413, .F. ) ;
#24072=CARTESIAN_POINT ( 'NONE',  ( 11.99451991528749417, 28.92564299267946382, 4.000000000000000000 ) ) ;
#24073=AXIS2_PLACEMENT_3D ( 'NONE', #2307, #122684, #23369 ) ;
#24074=CARTESIAN_POINT ( 'NONE',  ( 72.18398860626899705, 28.73617430169837661, 5.000000000000000000 ) ) ;
#24075=PLANE ( 'NONE',  #26018 ) ;
#24077=EDGE_CURVE ( 'NONE', #22612, #22841, #133276, .T. ) ;
#24078=CARTESIAN_POINT ( 'NONE',  ( -21.48921356237309155, -27.52281430457070499, 5.000000000000000000 ) ) ;
#24079=PLANE ( 'NONE',  #104524 ) ;
#24080=FACE_OUTER_BOUND ( 'NONE', #140654, .T. ) ;
#24081=DIRECTION ( 'NONE',  ( 0.6830127018922181881, 0.6830127018922202975, -0.2588190451025214056 ) ) ;
#24084=VECTOR ( 'NONE', #92300, 1000.000000000000114 ) ;
#24085=FACE_OUTER_BOUND ( 'NONE', #51856, .T. ) ;
#24087=ORIENTED_EDGE ( 'NONE', *, *, #136770, .T. ) ;
#24089=CARTESIAN_POINT ( 'NONE',  ( -25.64175702458845052, 15.75929247661555799, 19.34181609438705607 ) ) ;
#24090=EDGE_LOOP ( 'NONE', ( #73838, #93627, #101612 ) ) ;
#24091=VECTOR ( 'NONE', #107306, 999.9999999999998863 ) ;
#24092=VERTEX_POINT ( 'NONE', #99161 ) ;
#24093=ORIENTED_EDGE ( 'NONE', *, *, #104016, .F. ) ;
#24094=LINE ( 'NONE', #111059, #10863 ) ;
#24095=LINE ( 'NONE', #58920, #57863 ) ;
#24096=ORIENTED_EDGE ( 'NONE', *, *, #84863, .T. ) ;
#24100=DIRECTION ( 'NONE',  ( 0.7071067811865486830, -0.7071067811865464625, -0.000000000000000000 ) ) ;
#24102=CARTESIAN_POINT ( 'NONE',  ( -1.499999999999987566, 5.696342897626511359, -7.587980461218403860 ) ) ;
#24104=ORIENTED_EDGE ( 'NONE', *, *, #58313, .T. ) ;
#24105=EDGE_CURVE ( 'NONE', #107639, #127483, #89056, .T. ) ;
#24106=DIRECTION ( 'NONE',  ( -0.6830127018922180770, -0.6830127018922204085, -0.2588190451025213501 ) ) ;
#24108=LINE ( 'NONE', #79955, #62183 ) ;
#24109=CARTESIAN_POINT ( 'NONE',  ( -19.05000000000000071, 3.174999999999997158, 4.000000000000000000 ) ) ;
#24110=DIRECTION ( 'NONE',  ( -0.000000000000000000, -0.3543493200069152693, 0.9351131265310292928 ) ) ;
#24111=DIRECTION ( 'NONE',  ( 0.000000000000000000, 1.000000000000000000, -0.000000000000000000 ) ) ;
#24112=VECTOR ( 'NONE', #68438, 1000.000000000000000 ) ;
#24114=FACE_OUTER_BOUND ( 'NONE', #43275, .T. ) ;
#24115=VECTOR ( 'NONE', #74148, 1000.000000000000227 ) ;
#24116=DIRECTION ( 'NONE',  ( -0.3543493200069162685, -0.000000000000000000, -0.9351131265310288487 ) ) ;
#24117=ORIENTED_EDGE ( 'NONE', *, *, #107966, .T. ) ;
#24118=EDGE_LOOP ( 'NONE', ( #74263, #6428, #30308, #126804 ) ) ;
#24120=DIRECTION ( 'NONE',  ( 1.000000000000000000, 0.000000000000000000, 0.000000000000000000 ) ) ;
#24122=ORIENTED_EDGE ( 'NONE', *, *, #26113, .T. ) ;
#24123=CARTESIAN_POINT ( 'NONE',  ( 30.48921356237309510, -27.52281430457076894, 5.000000000000000000 ) ) ;
#24124=DIRECTION ( 'NONE',  ( -0.000000000000000000, 0.000000000000000000, 1.000000000000000000 ) ) ;
#24125=EDGE_CURVE ( 'NONE', #137134, #5098, #67298, .T. ) ;
#24127=ORIENTED_EDGE ( 'NONE', *, *, #11913, .T. ) ;
#24128=DIRECTION ( 'NONE',  ( 0.7071067811865486830, -0.7071067811865464625, -0.000000000000000000 ) ) ;
#24129=VERTEX_POINT ( 'NONE', #130413 ) ;
#24132=DIRECTION ( 'NONE',  ( 0.3543493200069162685, -0.000000000000000000, -0.9351131265310288487 ) ) ;
#24134=CARTESIAN_POINT ( 'NONE',  ( -14.99999999999990230, 7.559798855135676732, 4.979909187984716823 ) ) ;
#24136=EDGE_CURVE ( 'NONE', #40570, #98769, #75320, .T. ) ;
#24137=LINE ( 'NONE', #113265, #69653 ) ;
#24138=ORIENTED_EDGE ( 'NONE', *, *, #132025, .F. ) ;
#24139=FACE_OUTER_BOUND ( 'NONE', #26337, .T. ) ;
#24140=DIRECTION ( 'NONE',  ( -0.7071067811865486830, -0.7071067811865464625, 0.000000000000000000 ) ) ;
#24141=CARTESIAN_POINT ( 'NONE',  ( -34.92500000000001137, -21.72500000000000142, 0.4999999999999995559 ) ) ;
#24142=DIRECTION ( 'NONE',  ( -0.7071067811865487940, 0.7071067811865463515, -0.000000000000000000 ) ) ;
#24143=DIRECTION ( 'NONE',  ( -0.7071067811865486830, -0.7071067811865464625, 0.000000000000000000 ) ) ;
#24144=VERTEX_POINT ( 'NONE', #112228 ) ;
#24145=LINE ( 'NONE', #35773, #84706 ) ;
#24147=CARTESIAN_POINT ( 'NONE',  ( -7.214984197241858688, -3.740707523384244837, 15.76143240460122286 ) ) ;
#24148=DIRECTION ( 'NONE',  ( 0.6830127018922180770, -0.6830127018922204085, -0.2588190451025213501 ) ) ;
#24149=FACE_OUTER_BOUND ( 'NONE', #16320, .T. ) ;
#24151=ORIENTED_EDGE ( 'NONE', *, *, #129904, .T. ) ;
#24152=CARTESIAN_POINT ( 'NONE',  ( 59.99451991528749772, 28.92564299267980132, 4.000000000000000000 ) ) ;
#24153=EDGE_LOOP ( 'NONE', ( #104201, #51159, #34849, #135520 ) ) ;
#24154=VECTOR ( 'NONE', #20409, 1000.000000000000000 ) ;
#24156=VERTEX_POINT ( 'NONE', #81763 ) ;
#24158=LINE ( 'NONE', #45929, #131301 ) ;
#24159=EDGE_CURVE ( 'NONE', #56636, #60449, #70874, .T. ) ;
#24160=CARTESIAN_POINT ( 'NONE',  ( -33.18398860626899705, 28.73617430169810305, 5.000000000000000000 ) ) ;
#24161=DIRECTION ( 'NONE',  ( -0.3543493200069162685, -0.000000000000000000, -0.9351131265310288487 ) ) ;
#24162=FACE_BOUND ( 'NONE', #52009, .T. ) ;
#24163=DIRECTION ( 'NONE',  ( -0.6830127018922181881, 0.6830127018922202975, -0.2588190451025214056 ) ) ;
#24165=EDGE_CURVE ( 'NONE', #14419, #39873, #46282, .T. ) ;
#24167=DIRECTION ( 'NONE',  ( 0.6830127018922181881, 0.6830127018922202975, -0.2588190451025214056 ) ) ;
#24168=LINE ( 'NONE', #78557, #126825 ) ;
#24169=DIRECTION ( 'NONE',  ( -0.6830127018922180770, -0.6830127018922204085, -0.2588190451025213501 ) ) ;
#24170=ORIENTED_EDGE ( 'NONE', *, *, #42522, .T. ) ;
#24172=DIRECTION ( 'NONE',  ( -0.000000000000000000, 0.000000000000000000, 1.000000000000000000 ) ) ;
#24173=ORIENTED_EDGE ( 'NONE', *, *, #98334, .F. ) ;
#24174=ADVANCED_FACE ( 'NONE', ( #92578 ), #57160, .F. ) ;
#24175=EDGE_CURVE ( 'NONE', #83448, #12339, #134710, .T. ) ;
#24176=VECTOR ( 'NONE', #8030, 1000.000000000000227 ) ;
#24177=ORIENTED_EDGE ( 'NONE', *, *, #11337, .F. ) ;
#24179=ORIENTED_EDGE ( 'NONE', *, *, #46665, .F. ) ;
#24181=CARTESIAN_POINT ( 'NONE',  ( 11.99999999999991651, -15.03360074219758324, 5.000000000000000000 ) ) ;
#24182=VECTOR ( 'NONE', #43013, 1000.000000000000000 ) ;
#24183=ADVANCED_FACE ( 'NONE', ( #59986 ), #104155, .F. ) ;
#24185=DIRECTION ( 'NONE',  ( 0.6830127018922181881, 0.6830127018922202975, -0.2588190451025214056 ) ) ;
#24186=EDGE_CURVE ( 'NONE', #8228, #93313, #13583, .T. ) ;
#24187=( BOUNDED_CURVE ( )  B_SPLINE_CURVE ( 3, ( #142581, #133148, #43273, #33825 ),
 .UNSPECIFIED., .F., .F. ) 
 B_SPLINE_CURVE_WITH_KNOTS ( ( 4, 4 ),
 ( 1.901594255663605182, 1.933014472006542306 ),
 .UNSPECIFIED. ) 
 CURVE ( )  GEOMETRIC_REPRESENTATION_ITEM ( )  RATIONAL_B_SPLINE_CURVE ( ( 1.000000000000000000, 0.9999177325257868620, 0.9999177325257868620, 1.000000000000000000 ) ) 
 REPRESENTATION_ITEM ( '' )  );
#24188=CARTESIAN_POINT ( 'NONE',  ( -39.18398860626899705, 28.73617430169814568, 5.000000000000000000 ) ) ;
#24189=EDGE_CURVE ( 'NONE', #92779, #57095, #2724, .T. ) ;
#24190=CARTESIAN_POINT ( 'NONE',  ( 8.510786437626906675, -27.52281430457049183, 5.000000000000000000 ) ) ;
#24191=VECTOR ( 'NONE', #35324, 1000.000000000000000 ) ;
#24193=PLANE ( 'NONE',  #69019 ) ;
#24194=PLANE ( 'NONE',  #38007 ) ;
#24195=CARTESIAN_POINT ( 'NONE',  ( 27.29974487139158512, -27.71228299555225405, 4.000000000000000000 ) ) ;
#24196=PLANE ( 'NONE',  #81005 ) ;
#24197=EDGE_LOOP ( 'NONE', ( #109550, #66485, #91576, #128104 ) ) ;
#24198=ORIENTED_EDGE ( 'NONE', *, *, #133712, .F. ) ;
#24199=CARTESIAN_POINT ( 'NONE',  ( 25.00442415654155681, 3.591886032380943838, 4.000000000000000000 ) ) ;
#24200=( BOUNDED_CURVE ( )  B_SPLINE_CURVE ( 3, ( #83223, #70938, #94077, #36161 ),
 .UNSPECIFIED., .F., .T. ) 
 B_SPLINE_CURVE_WITH_KNOTS ( ( 4, 4 ),
 ( 4.350170835173027939, 4.500739107949266682 ),
 .UNSPECIFIED. ) 
 CURVE ( )  GEOMETRIC_REPRESENTATION_ITEM ( )  RATIONAL_B_SPLINE_CURVE ( ( 1.000000000000000000, 0.9981116584018943083, 0.9981116584018943083, 1.000000000000000000 ) ) 
 REPRESENTATION_ITEM ( '' )  );
#24201=FACE_OUTER_BOUND ( 'NONE', #111150, .T. ) ;
#24202=ORIENTED_EDGE ( 'NONE', *, *, #94224, .T. ) ;
#24203=EDGE_CURVE ( 'NONE', #23833, #32348, #119157, .T. ) ;
#24204=ORIENTED_EDGE ( 'NONE', *, *, #137850, .F. ) ;
#24206=DIRECTION ( 'NONE',  ( 1.000000000000000000, 0.000000000000000000, 0.000000000000000000 ) ) ;
#24207=ORIENTED_EDGE ( 'NONE', *, *, #143397, .T. ) ;
#24208=LINE ( 'NONE', #33675, #6907 ) ;
#24209=ADVANCED_FACE ( 'NONE', ( #48380 ), #69444, .T. ) ;
#24210=VECTOR ( 'NONE', #137600, 1000.000000000000000 ) ;
#24214=VECTOR ( 'NONE', #49219, 1000.000000000000000 ) ;
#24215=FACE_OUTER_BOUND ( 'NONE', #127300, .T. ) ;
#24216=ORIENTED_EDGE ( 'NONE', *, *, #39775, .F. ) ;
#24217=VECTOR ( 'NONE', #118827, 1000.000000000000000 ) ;
#24218=LINE ( 'NONE', #14019, #131441 ) ;
#24219=LINE ( 'NONE', #124939, #39714 ) ;
#24220=CARTESIAN_POINT ( 'NONE',  ( -15.70710678118642711, -6.740707523384211086, 5.000000000000000000 ) ) ;
#24221=CARTESIAN_POINT ( 'NONE',  ( -19.39656807105345848, -14.24070752338412937, 19.24067776001721342 ) ) ;
#24222=ORIENTED_EDGE ( 'NONE', *, *, #142388, .T. ) ;
#24223=ORIENTED_EDGE ( 'NONE', *, *, #106454, .T. ) ;
#24224=DIRECTION ( 'NONE',  ( 1.000000000000000000, 0.000000000000000000, 0.000000000000000000 ) ) ;
#24225=CARTESIAN_POINT ( 'NONE',  ( -31.49999999999977973, 0.4497235411627178991, -5.599840258123613523 ) ) ;
#24226=ORIENTED_EDGE ( 'NONE', *, *, #54493, .F. ) ;
#24228=EDGE_CURVE ( 'NONE', #114524, #96272, #102666, .T. ) ;
#24229=PLANE ( 'NONE',  #110408 ) ;
#24230=ADVANCED_FACE ( 'NONE', ( #133964 ), #137547, .F. ) ;
#24233=FACE_OUTER_BOUND ( 'NONE', #108436, .T. ) ;
#24234=CARTESIAN_POINT ( 'NONE',  ( 54.48921356237310221, -27.52281430457093236, 5.000000000000000000 ) ) ;
#24235=LINE ( 'NONE', #111967, #86402 ) ;
#24237=CARTESIAN_POINT ( 'NONE',  ( -23.99999999999982592, 17.58746187583906107, 4.000000000000000000 ) ) ;
#24238=CARTESIAN_POINT ( 'NONE',  ( 34.49999999999975842, 16.77039438581782349, 0.4657186855306942319 ) ) ;
#24239=CARTESIAN_POINT ( 'NONE',  ( -30.33010218547246950, 17.25929247661554555, 19.83885114516078474 ) ) ;
#24240=EDGE_LOOP ( 'NONE', ( #51513, #62975, #33531, #91148 ) ) ;
#24241=ORIENTED_EDGE ( 'NONE', *, *, #72179, .F. ) ;
#24242=CARTESIAN_POINT ( 'NONE',  ( -26.99999999999980460, 8.587461875839162317, 4.000000000000000000 ) ) ;
#24243=CARTESIAN_POINT ( 'NONE',  ( -32.99999999999977263, -10.77435723561698566, -9.972017380717154822 ) ) ;
#24245=DIRECTION ( 'NONE',  ( 0.7071067811865486830, -0.7071067811865464625, -0.000000000000000000 ) ) ;
#24246=ORIENTED_EDGE ( 'NONE', *, *, #82734, .F. ) ;
#24247=DIRECTION ( 'NONE',  ( 2.781805975412905274E-17, -0.3543493200069152138, 0.9351131265310292928 ) ) ;
#24248=LINE ( 'NONE', #101797, #85325 ) ;
#24249=DIRECTION ( 'NONE',  ( -0.6830127018922181881, 0.6830127018922202975, -0.2588190451025214056 ) ) ;
#24251=EDGE_CURVE ( 'NONE', #76457, #65481, #6964, .T. ) ;
#24252=DIRECTION ( 'NONE',  ( 0.7071067811865487940, 0.7071067811865463515, 0.000000000000000000 ) ) ;
#24253=LINE ( 'NONE', #133040, #114104 ) ;
#24255=VECTOR ( 'NONE', #86953, 999.9999999999998863 ) ;
#24256=CARTESIAN_POINT ( 'NONE',  ( 14.99451991528749595, 28.92564299267948513, 4.000000000000000000 ) ) ;
#24257=CARTESIAN_POINT ( 'NONE',  ( -9.792893218813391698, 9.759292476615618384, 5.000000000000000000 ) ) ;
#24258=CARTESIAN_POINT ( 'NONE',  ( -34.49999999999976552, -14.94567065516890558, 4.994342998332162331 ) ) ;
#24262=CARTESIAN_POINT ( 'NONE',  ( -21.29974487139158512, -27.71228299555221142, 4.000000000000000000 ) ) ;
#24264=CARTESIAN_POINT ( 'NONE',  ( -0.4892135623730947680, -27.52281430457055578, 5.000000000000000000 ) ) ;
#24266=EDGE_CURVE ( 'NONE', #119390, #115334, #82451, .T. ) ;
#24267=DIRECTION ( 'NONE',  ( -0.000000000000000000, 0.000000000000000000, 1.000000000000000000 ) ) ;
#24268=DIRECTION ( 'NONE',  ( 0.000000000000000000, 0.000000000000000000, 1.000000000000000000 ) ) ;
#24269=ORIENTED_EDGE ( 'NONE', *, *, #130272, .F. ) ;
#24270=ORIENTED_EDGE ( 'NONE', *, *, #346, .T. ) ;
#24271=CARTESIAN_POINT ( 'NONE',  ( -8.999999999999921840, -16.06887692260765377, 4.000000000000000000 ) ) ;
#24274=DIRECTION ( 'NONE',  ( 0.3543493200069162685, -0.000000000000000000, -0.9351131265310288487 ) ) ;
#24276=PLANE ( 'NONE',  #106515 ) ;
#24278=EDGE_CURVE ( 'NONE', #34100, #50218, #104899, .T. ) ;
#24279=DIRECTION ( 'NONE',  ( 0.7071067811865487940, 0.7071067811865463515, -0.000000000000000000 ) ) ;
#24280=ORIENTED_EDGE ( 'NONE', *, *, #104473, .F. ) ;
#24282=CARTESIAN_POINT ( 'NONE',  ( -15.18398860626900237, 28.73617430169797871, 5.000000000000000000 ) ) ;
#24284=DIRECTION ( 'NONE',  ( -0.7071067811865486830, -0.7071067811865464625, 0.000000000000000000 ) ) ;
#24285=DIRECTION ( 'NONE',  ( -0.7071067811865486830, -0.7071067811865464625, 0.000000000000000000 ) ) ;
#24286=ORIENTED_EDGE ( 'NONE', *, *, #134834, .F. ) ;
#24287=EDGE_CURVE ( 'NONE', #54574, #92154, #17860, .T. ) ;
#24288=FACE_OUTER_BOUND ( 'NONE', #49017, .T. ) ;
#24291=CARTESIAN_POINT ( 'NONE',  ( 16.82816939922341604, 18.75929247661552424, 4.000000000000000000 ) ) ;
#24293=ORIENTED_EDGE ( 'NONE', *, *, #48422, .T. ) ;
#24294=ORIENTED_EDGE ( 'NONE', *, *, #57740, .T. ) ;
#24295=LINE ( 'NONE', #68541, #29162 ) ;
#24298=ADVANCED_FACE ( 'NONE', ( #49122 ), #41074, .T. ) ;
#24299=CARTESIAN_POINT ( 'NONE',  ( -29.75830541574794808, 0.7592924766157173044, 14.37146558664989904 ) ) ;
#24300=LINE ( 'NONE', #81568, #126303 ) ;
#24301=ORIENTED_EDGE ( 'NONE', *, *, #11779, .T. ) ;
#24302=CARTESIAN_POINT ( 'NONE',  ( -20.29289321881331176, -18.74070752338409562, 5.000000000000000000 ) ) ;
#24303=CARTESIAN_POINT ( 'NONE',  ( -2.018447346356678995, 18.75929247661552424, 20.33588619593443170 ) ) ;
#24305=DIRECTION ( 'NONE',  ( -0.000000000000000000, 0.000000000000000000, 1.000000000000000000 ) ) ;
#24306=EDGE_LOOP ( 'NONE', ( #19472, #76371, #111926, #22409 ) ) ;
#24311=VECTOR ( 'NONE', #33854, 1000.000000000000000 ) ;
#24312=ORIENTED_EDGE ( 'NONE', *, *, #5812, .F. ) ;
#24313=VECTOR ( 'NONE', #2001, 1000.000000000000000 ) ;
#24314=CARTESIAN_POINT ( 'NONE',  ( -29.99999999999979750, 14.87792677143805520, -11.06722581663446903 ) ) ;
#24315=DIRECTION ( 'NONE',  ( -0.7071067811865487940, 0.7071067811865463515, -0.000000000000000000 ) ) ;
#24317=CARTESIAN_POINT ( 'NONE',  ( 15.78162688292483473, 21.74787736706806029, 4.999607392498049308 ) ) ;
#24318=DIRECTION ( 'NONE',  ( -0.6830127018922180770, -0.6830127018922204085, -0.2588190451025213501 ) ) ;
#24319=EDGE_LOOP ( 'NONE', ( #66076, #22965, #52344, #97397 ) ) ;
#24320=ORIENTED_EDGE ( 'NONE', *, *, #39790, .F. ) ;
#24321=DIRECTION ( 'NONE',  ( -0.3543493200069162685, -0.000000000000000000, -0.9351131265310288487 ) ) ;
#24323=ORIENTED_EDGE ( 'NONE', *, *, #59393, .T. ) ;
#24324=LINE ( 'NONE', #26468, #109247 ) ;
#24325=CARTESIAN_POINT ( 'NONE',  ( -34.92500000000001137, -6.183345613589518841, 4.500000000000000888 ) ) ;
#24326=FACE_OUTER_BOUND ( 'NONE', #22454, .T. ) ;
#24327=VERTEX_POINT ( 'NONE', #28789 ) ;
#24328=FACE_BOUND ( 'NONE', #64160, .T. ) ;
#24330=CARTESIAN_POINT ( 'NONE',  ( -21.48921356237309155, -27.52281430457070499, 5.000000000000000000 ) ) ;
#24331=DIRECTION ( 'NONE',  ( -0.7071067811865486830, -0.7071067811865464625, -0.000000000000000000 ) ) ;
#24332=DIRECTION ( 'NONE',  ( -0.7071067811865486830, -0.7071067811865464625, 0.000000000000000000 ) ) ;
#24333=DIRECTION ( 'NONE',  ( 0.7071067811865486830, -0.7071067811865464625, -0.000000000000000000 ) ) ;
#24335=ORIENTED_EDGE ( 'NONE', *, *, #126321, .T. ) ;
#24336=EDGE_CURVE ( 'NONE', #86181, #2775, #51966, .T. ) ;
#24339=ORIENTED_EDGE ( 'NONE', *, *, #8369, .T. ) ;
#24340=EDGE_CURVE ( 'NONE', #73530, #114745, #17185, .T. ) ;
#24341=LINE ( 'NONE', #91058, #129949 ) ;
#24342=ORIENTED_EDGE ( 'NONE', *, *, #40425, .F. ) ;
#24343=ADVANCED_FACE ( 'NONE', ( #96145 ), #106289, .F. ) ;
#24344=DIRECTION ( 'NONE',  ( -0.000000000000000000, 0.3543493200069153248, 0.9351131265310292928 ) ) ;
#24345=ADVANCED_FACE ( 'NONE', ( #84595 ), #29470, .F. ) ;
#24346=DIRECTION ( 'NONE',  ( -0.7071067811865486830, -0.7071067811865464625, -0.000000000000000000 ) ) ;
#24347=DIRECTION ( 'NONE',  ( -0.7071067811865487940, 0.7071067811865463515, -0.000000000000000000 ) ) ;
#24348=ORIENTED_EDGE ( 'NONE', *, *, #93283, .T. ) ;
#24350=LINE ( 'NONE', #2574, #70953 ) ;
#24351=EDGE_CURVE ( 'NONE', #8640, #50635, #107739, .T. ) ;
#24353=CARTESIAN_POINT ( 'NONE',  ( -15.51665438641034989, 22.22500000000000142, 4.500000000000000888 ) ) ;
#24354=DIRECTION ( 'NONE',  ( -0.3543493200069162685, -0.000000000000000000, -0.9351131265310288487 ) ) ;
#24355=CARTESIAN_POINT ( 'NONE',  ( 13.63753812416088707, 22.22500000000000142, 4.000000000000000000 ) ) ;
#24356=ORIENTED_EDGE ( 'NONE', *, *, #86841, .T. ) ;
#24357=CARTESIAN_POINT ( 'NONE',  ( 16.49999999999988276, -10.04351517176476527, -1.623559851933785714 ) ) ;
#24358=LINE ( 'NONE', #1153, #62781 ) ;
#24359=ADVANCED_FACE ( 'NONE', ( #16437 ), #94011, .T. ) ;
#24360=ORIENTED_EDGE ( 'NONE', *, *, #4311, .T. ) ;
#24361=ORIENTED_EDGE ( 'NONE', *, *, #4451, .F. ) ;
#24362=EDGE_CURVE ( 'NONE', #65251, #20682, #116495, .T. ) ;
#24365=EDGE_LOOP ( 'NONE', ( #111901, #2692, #141057, #108066 ) ) ;
#24366=( BOUNDED_CURVE ( )  B_SPLINE_CURVE ( 3, ( #33569, #22618, #66885, #112522 ),
 .UNSPECIFIED., .F., .T. ) 
 B_SPLINE_CURVE_WITH_KNOTS ( ( 4, 4 ),
 ( 2.001653308786151442, 3.503810798801451742 ),
 .UNSPECIFIED. ) 
 CURVE ( )  GEOMETRIC_REPRESENTATION_ITEM ( )  RATIONAL_B_SPLINE_CURVE ( ( 1.000000000000000000, 0.8206354192515199486, 0.8206354192515199486, 1.000000000000000000 ) ) 
 REPRESENTATION_ITEM ( '' )  );
#24367=EDGE_CURVE ( 'NONE', #42968, #29293, #39675, .T. ) ;
#24368=DIRECTION ( 'NONE',  ( 0.6830127018922181881, 0.6830127018922202975, -0.2588190451025214056 ) ) ;
#24369=VECTOR ( 'NONE', #85807, 1000.000000000000000 ) ;
#24372=CARTESIAN_POINT ( 'NONE',  ( -29.99999999999978328, 1.552185695429149304, 5.000000000000000000 ) ) ;
#24373=ORIENTED_EDGE ( 'NONE', *, *, #33298, .F. ) ;
#24375=CARTESIAN_POINT ( 'NONE',  ( 21.29974487139158512, -27.71228299555221142, 4.000000000000000000 ) ) ;
#24376=EDGE_LOOP ( 'NONE', ( #8779, #8893, #140460, #72393 ) ) ;
#24377=CARTESIAN_POINT ( 'NONE',  ( 30.18398860626900060, 28.73617430169808173, 5.000000000000000000 ) ) ;
#24378=DIRECTION ( 'NONE',  ( 0.3543493200069163240, -0.000000000000000000, 0.9351131265310288487 ) ) ;
#24379=VERTEX_POINT ( 'NONE', #122183 ) ;
#24380=FACE_OUTER_BOUND ( 'NONE', #116533, .T. ) ;
#24381=CARTESIAN_POINT ( 'NONE',  ( -16.49999999999988276, 13.56627193232213102, -10.57019076586072259 ) ) ;
#24383=ORIENTED_EDGE ( 'NONE', *, *, #128484, .F. ) ;
#24384=DIRECTION ( 'NONE',  ( 0.7071067811865486830, -0.7071067811865464625, -0.000000000000000000 ) ) ;
#24385=AXIS2_PLACEMENT_3D ( 'NONE', #69576, #26046, #37650 ) ;
#24386=ORIENTED_EDGE ( 'NONE', *, *, #74648, .F. ) ;
#24387=ORIENTED_EDGE ( 'NONE', *, *, #43077, .T. ) ;
#24388=VERTEX_POINT ( 'NONE', #99007 ) ;
#24389=EDGE_CURVE ( 'NONE', #101006, #90591, #30932, .T. ) ;
#24392=DIRECTION ( 'NONE',  ( -0.6830127018922181881, 0.6830127018922202975, -0.2588190451025214056 ) ) ;
#24393=LINE ( 'NONE', #3333, #92831 ) ;
#24394=VERTEX_POINT ( 'NONE', #8399 ) ;
#24396=EDGE_CURVE ( 'NONE', #69437, #98488, #22155, .T. ) ;
#24397=VECTOR ( 'NONE', #57309, 1000.000000000000000 ) ;
#24399=LINE ( 'NONE', #68646, #106391 ) ;
#24400=VECTOR ( 'NONE', #133426, 1000.000000000000000 ) ;
#24401=LINE ( 'NONE', #100549, #76130 ) ;
#24402=VECTOR ( 'NONE', #13291, 1000.000000000000227 ) ;
#24403=LINE ( 'NONE', #14240, #35151 ) ;
#24404=ORIENTED_EDGE ( 'NONE', *, *, #15741, .F. ) ;
#24405=ORIENTED_EDGE ( 'NONE', *, *, #62800, .F. ) ;
#24407=ORIENTED_EDGE ( 'NONE', *, *, #101070, .T. ) ;
#24412=CARTESIAN_POINT ( 'NONE',  ( 0.000000000000000000, 0.000000000000000000, 5.000000000000000000 ) ) ;
#24413=DIRECTION ( 'NONE',  ( -0.7071067811865487940, 0.7071067811865463515, -0.000000000000000000 ) ) ;
#24415=PLANE ( 'NONE',  #110900 ) ;
#24416=DIRECTION ( 'NONE',  ( 0.7071067811865486830, -0.7071067811865464625, -0.000000000000000000 ) ) ;
#24417=EDGE_CURVE ( 'NONE', #106976, #69406, #130963, .T. ) ;
#24418=CARTESIAN_POINT ( 'NONE',  ( 19.49999999999987921, 13.56627193232217188, -10.57019076586064266 ) ) ;
#24421=ORIENTED_EDGE ( 'NONE', *, *, #113073, .F. ) ;
#24422=DIRECTION ( 'NONE',  ( 0.7071067811865487940, 0.7071067811865463515, -0.000000000000000000 ) ) ;
#24423=ORIENTED_EDGE ( 'NONE', *, *, #27960, .T. ) ;
#24424=FACE_OUTER_BOUND ( 'NONE', #98997, .T. ) ;
#24425=CARTESIAN_POINT ( 'NONE',  ( 18.70701326429291456, -21.74070752338405654, 4.999753212805210012 ) ) ;
#24426=VERTEX_POINT ( 'NONE', #32349 ) ;
#24428=DIRECTION ( 'NONE',  ( -0.7071067811865487940, 0.7071067811865463515, -0.000000000000000000 ) ) ;
#24429=EDGE_CURVE ( 'NONE', #5483, #37692, #31635, .T. ) ;
#24430=ORIENTED_EDGE ( 'NONE', *, *, #32868, .T. ) ;
#24431=DIRECTION ( 'NONE',  ( 0.3543493200069162685, -0.000000000000000000, -0.9351131265310288487 ) ) ;
#24432=EDGE_LOOP ( 'NONE', ( #136582, #64651, #135205, #133382 ) ) ;
#24433=DIRECTION ( 'NONE',  ( -0.6830127018922181881, 0.6830127018922202975, -0.2588190451025214056 ) ) ;
#24434=VERTEX_POINT ( 'NONE', #53372 ) ;
#24435=CARTESIAN_POINT ( 'NONE',  ( 45.29974487139158867, -27.71228299555237840, 4.000000000000000000 ) ) ;
#24437=LINE ( 'NONE', #68685, #64865 ) ;
#24438=CARTESIAN_POINT ( 'NONE',  ( 36.18398860626899705, 28.73617430169812437, 5.000000000000000000 ) ) ;
#24439=EDGE_LOOP ( 'NONE', ( #121271, #140270, #44785, #114858 ) ) ;
#24440=DIRECTION ( 'NONE',  ( 0.6830127018922180770, -0.6830127018922204085, -0.2588190451025213501 ) ) ;
#24441=CARTESIAN_POINT ( 'NONE',  ( 0.4892135623730947680, -27.52281430457055578, 5.000000000000000000 ) ) ;
#24442=CARTESIAN_POINT ( 'NONE',  ( 12.18398860626900060, 28.73617430169795739, 5.000000000000000000 ) ) ;
#24445=CARTESIAN_POINT ( 'NONE',  ( -12.48921356237309155, -27.52281430457064104, 5.000000000000000000 ) ) ;
#24446=DIRECTION ( 'NONE',  ( 0.6830127018922180770, -0.6830127018922204085, -0.2588190451025213501 ) ) ;
#24447=ORIENTED_EDGE ( 'NONE', *, *, #26988, .T. ) ;
#24448=EDGE_CURVE ( 'NONE', #141174, #6489, #130245, .T. ) ;
#24449=DIRECTION ( 'NONE',  ( -0.7071067811865486830, -0.7071067811865464625, -0.000000000000000000 ) ) ;
#24450=ORIENTED_EDGE ( 'NONE', *, *, #132450, .T. ) ;
#24451=EDGE_CURVE ( 'NONE', #41816, #113815, #143243, .T. ) ;
#24453=DIRECTION ( 'NONE',  ( -0.7071067811865486830, 0.7071067811865464625, 0.000000000000000000 ) ) ;
#24456=VERTEX_POINT ( 'NONE', #75167 ) ;
#24457=CARTESIAN_POINT ( 'NONE',  ( -14.99451991528749595, 28.92564299267948513, 4.000000000000000000 ) ) ;
#24458=CARTESIAN_POINT ( 'NONE',  ( 2.277185695429367662, -21.72499999999999432, 5.000000000000000000 ) ) ;
#24460=EDGE_CURVE ( 'NONE', #51050, #74995, #52656, .T. ) ;
#24461=ORIENTED_EDGE ( 'NONE', *, *, #51679, .F. ) ;
#24462=DIRECTION ( 'NONE',  ( 0.7071067811865486830, -0.7071067811865464625, -0.000000000000000000 ) ) ;
#24463=EDGE_CURVE ( 'NONE', #82613, #92516, #9103, .T. ) ;
#24464=FACE_OUTER_BOUND ( 'NONE', #112111, .T. ) ;
#24466=VERTEX_POINT ( 'NONE', #33100 ) ;
#24467=CARTESIAN_POINT ( 'NONE',  ( 34.92499999999998295, -16.29806943317885271, 4.500000000000000888 ) ) ;
#24469=CARTESIAN_POINT ( 'NONE',  ( 14.51078643762690490, -27.52281430457045275, 5.000000000000000000 ) ) ;
#24470=DIRECTION ( 'NONE',  ( -0.7071067811865487940, 0.7071067811865463515, -0.000000000000000000 ) ) ;
#24471=CARTESIAN_POINT ( 'NONE',  ( 8.292893218813407685, -3.740707523384241728, 5.000000000000000000 ) ) ;
#24472=EDGE_LOOP ( 'NONE', ( #82351, #53951, #140450, #26125 ) ) ;
#24473=VECTOR ( 'NONE', #40555, 1000.000000000000000 ) ;
#24474=EDGE_LOOP ( 'NONE', ( #64671, #128686, #4711, #130771 ) ) ;
#24477=ORIENTED_EDGE ( 'NONE', *, *, #132966, .F. ) ;
#24478=VECTOR ( 'NONE', #55528, 1000.000000000000000 ) ;
#24479=CARTESIAN_POINT ( 'NONE',  ( -22.17183060077631396, 18.75929247661552779, 4.000000000000000000 ) ) ;
#24480=DIRECTION ( 'NONE',  ( -0.000000000000000000, -0.3543493200069152693, 0.9351131265310292928 ) ) ;
#24483=ORIENTED_EDGE ( 'NONE', *, *, #86189, .F. ) ;
#24484=EDGE_CURVE ( 'NONE', #20411, #83949, #141838, .T. ) ;
#24485=DIRECTION ( 'NONE',  ( -0.7071067811865486830, -0.7071067811865464625, -0.000000000000000000 ) ) ;
#24486=LINE ( 'NONE', #112923, #130036 ) ;
#24487=CARTESIAN_POINT ( 'NONE',  ( 23.99451991528749062, 28.92564299267954908, 4.000000000000000000 ) ) ;
#24489=ORIENTED_EDGE ( 'NONE', *, *, #55465, .T. ) ;
#24490=CARTESIAN_POINT ( 'NONE',  ( -18.48921356237309510, -27.52281430457068367, 5.000000000000000000 ) ) ;
#24491=LINE ( 'NONE', #91219, #14504 ) ;
#24493=ORIENTED_EDGE ( 'NONE', *, *, #68463, .T. ) ;
#24494=CARTESIAN_POINT ( 'NONE',  ( 0.000000000000000000, 21.72500000000000142, 4.500000000000000888 ) ) ;
#24496=PLANE ( 'NONE',  #60514 ) ;
#24497=DIRECTION ( 'NONE',  ( 0.7071067811865486830, -0.7071067811865464625, -0.000000000000000000 ) ) ;
#24499=CARTESIAN_POINT ( 'NONE',  ( 30.70710678118633297, 8.259292476615637923, 5.000000000000000000 ) ) ;
#24500=FACE_OUTER_BOUND ( 'NONE', #130732, .T. ) ;
#24502=VECTOR ( 'NONE', #6601, 1000.000000000000227 ) ;
#24503=EDGE_CURVE ( 'NONE', #98842, #75802, #67120, .T. ) ;
#24504=ORIENTED_EDGE ( 'NONE', *, *, #56229, .F. ) ;
#24505=AXIS2_PLACEMENT_3D ( 'NONE', #9711, #18422, #61996 ) ;
#24506=ORIENTED_EDGE ( 'NONE', *, *, #89045, .T. ) ;
#24507=ADVANCED_FACE ( 'NONE', ( #120022 ), #110586, .F. ) ;
#24509=DIRECTION ( 'NONE',  ( 1.000000000000000000, 0.000000000000000000, 0.000000000000000000 ) ) ;
#24510=ORIENTED_EDGE ( 'NONE', *, *, #72587, .F. ) ;
#24511=ORIENTED_EDGE ( 'NONE', *, *, #78689, .F. ) ;
#24512=VECTOR ( 'NONE', #107836, 1000.000000000000227 ) ;
#24513=EDGE_CURVE ( 'NONE', #20118, #76695, #9864, .T. ) ;
#24514=EDGE_CURVE ( 'NONE', #103671, #8470, #98326, .T. ) ;
#24515=LINE ( 'NONE', #4120, #24313 ) ;
#24518=DIRECTION ( 'NONE',  ( -0.7071067811865486830, -0.7071067811865464625, 0.000000000000000000 ) ) ;
#24519=CARTESIAN_POINT ( 'NONE',  ( -20.99999999999985079, -6.108550654416979420, -3.114665004255016356 ) ) ;
#24520=DIRECTION ( 'NONE',  ( -0.7071067811865486830, -0.7071067811865464625, -0.000000000000000000 ) ) ;
#24521=ORIENTED_EDGE ( 'NONE', *, *, #71587, .F. ) ;
#24522=CARTESIAN_POINT ( 'NONE',  ( 9.328169399223463998, -21.74070752338406365, 4.000000000000000000 ) ) ;
#24523=EDGE_CURVE ( 'NONE', #77379, #9354, #142547, .T. ) ;
#24524=ORIENTED_EDGE ( 'NONE', *, *, #11433, .T. ) ;
#24525=DIRECTION ( 'NONE',  ( -0.000000000000000000, 0.000000000000000000, 1.000000000000000000 ) ) ;
#24526=ORIENTED_EDGE ( 'NONE', *, *, #114676, .F. ) ;
#24527=DIRECTION ( 'NONE',  ( -0.7071067811865487940, 0.7071067811865463515, -0.000000000000000000 ) ) ;
#24528=ADVANCED_FACE ( 'NONE', ( #87451 ), #76589, .T. ) ;
#24529=ORIENTED_EDGE ( 'NONE', *, *, #104545, .T. ) ;
#24531=VERTEX_POINT ( 'NONE', #80861 ) ;
#24532=VERTEX_POINT ( 'NONE', #103287 ) ;
#24533=ORIENTED_EDGE ( 'NONE', *, *, #23124, .F. ) ;
#24534=EDGE_CURVE ( 'NONE', #42223, #55852, #20068, .T. ) ;
#24537=CARTESIAN_POINT ( 'NONE',  ( 12.43680103220821742, -12.74070752338415069, 9.898150129686346332 ) ) ;
#24538=CARTESIAN_POINT ( 'NONE',  ( 2.999999999999977351, -21.84840872380824095, 2.849755605029614447 ) ) ;
#24540=PLANE ( 'NONE',  #72931 ) ;
#24541=DIRECTION ( 'NONE',  ( -0.7071067811865486830, -0.7071067811865464625, 0.000000000000000000 ) ) ;
#24542=DIRECTION ( 'NONE',  ( -0.7071067811865486830, -0.7071067811865464625, 0.000000000000000000 ) ) ;
#24543=EDGE_CURVE ( 'NONE', #68447, #89873, #114176, .T. ) ;
#24544=VECTOR ( 'NONE', #57296, 1000.000000000000000 ) ;
#24545=CARTESIAN_POINT ( 'NONE',  ( 34.78501580275788996, -3.740707523384241728, 15.76143240460132411 ) ) ;
#24548=LINE ( 'NONE', #23849, #57329 ) ;
#24549=CARTESIAN_POINT ( 'NONE',  ( 0.000000000000000000, 0.000000000000000000, 5.000000000000000000 ) ) ;
#24550=ORIENTED_EDGE ( 'NONE', *, *, #91788, .F. ) ;
#24551=ORIENTED_EDGE ( 'NONE', *, *, #8883, .T. ) ;
#24552=ADVANCED_FACE ( 'NONE', ( #100464 ), #125051, .F. ) ;
#24553=LINE ( 'NONE', #14399, #37994 ) ;
#24554=EDGE_LOOP ( 'NONE', ( #61711, #92279, #100762, #87674 ) ) ;
#24555=CARTESIAN_POINT ( 'NONE',  ( -11.99999999999990763, 1.552185695429147527, 5.000000000000000000 ) ) ;
#24556=DIRECTION ( 'NONE',  ( 0.7071067811865487940, -0.7071067811865463515, 0.000000000000000000 ) ) ;
#24558=DIRECTION ( 'NONE',  ( -0.7071067811865486830, -0.7071067811865464625, -0.000000000000000000 ) ) ;
#24559=CARTESIAN_POINT ( 'NONE',  ( 0.000000000000000000, 0.000000000000000000, 5.000000000000000000 ) ) ;
#24561=ORIENTED_EDGE ( 'NONE', *, *, #5312, .T. ) ;
#24562=ADVANCED_FACE ( 'NONE', ( #135933 ), #56981, .F. ) ;
#24563=FACE_OUTER_BOUND ( 'NONE', #39992, .T. ) ;
#24565=CARTESIAN_POINT ( 'NONE',  ( -32.99451991528749062, 28.92564299267960948, 4.000000000000000000 ) ) ;
#24566=EDGE_CURVE ( 'NONE', #63744, #140742, #14140, .T. ) ;
#24569=ORIENTED_EDGE ( 'NONE', *, *, #28321, .T. ) ;
#24570=CARTESIAN_POINT ( 'NONE',  ( 6.516654386410396071, 22.22500000000000142, 4.500000000000000888 ) ) ;
#24571=VECTOR ( 'NONE', #50015, 1000.000000000000000 ) ;
#24572=CARTESIAN_POINT ( 'NONE',  ( 24.18398860626899705, 28.73617430169804265, 5.000000000000000000 ) ) ;
#24573=ORIENTED_EDGE ( 'NONE', *, *, #15161, .F. ) ;
#24574=EDGE_LOOP ( 'NONE', ( #35144, #44229, #26867, #52487 ) ) ;
#24575=ORIENTED_EDGE ( 'NONE', *, *, #4901, .F. ) ;
#24576=DIRECTION ( 'NONE',  ( -0.7071067811865486830, -0.7071067811865464625, -0.000000000000000000 ) ) ;
#24577=DIRECTION ( 'NONE',  ( 0.7071067811865487940, 0.7071067811865463515, 0.000000000000000000 ) ) ;
#24578=CARTESIAN_POINT ( 'NONE',  ( -54.48921356237310221, -27.52281430457093236, 5.000000000000000000 ) ) ;
#24579=LINE ( 'NONE', #77570, #42731 ) ;
#24580=( BOUNDED_CURVE ( )  B_SPLINE_CURVE ( 3, ( #83651, #16180, #60472, #127858 ),
 .UNSPECIFIED., .F., .F. ) 
 B_SPLINE_CURVE_WITH_KNOTS ( ( 4, 4 ),
 ( 4.350170835173026163, 4.500739107949264906 ),
 .UNSPECIFIED. ) 
 CURVE ( )  GEOMETRIC_REPRESENTATION_ITEM ( )  RATIONAL_B_SPLINE_CURVE ( ( 1.000000000000000000, 0.9981116584018943083, 0.9981116584018943083, 1.000000000000000000 ) ) 
 REPRESENTATION_ITEM ( '' )  );
#24581=ORIENTED_EDGE ( 'NONE', *, *, #56708, .F. ) ;
#24582=VECTOR ( 'NONE', #41548, 1000.000000000000000 ) ;
#24583=ADVANCED_FACE ( 'NONE', ( #58433 ), #35941, .T. ) ;
#24584=LINE ( 'NONE', #66683, #132233 ) ;
#24585=FACE_OUTER_BOUND ( 'NONE', #37691, .T. ) ;
#24586=ORIENTED_EDGE ( 'NONE', *, *, #61936, .T. ) ;
#24587=DIRECTION ( 'NONE',  ( -0.7071067811865486830, -0.7071067811865464625, 0.000000000000000000 ) ) ;
#24588=EDGE_LOOP ( 'NONE', ( #109728, #43109, #132825, #124586, #71597, #58637 ) ) ;
#24589=DIRECTION ( 'NONE',  ( 0.7071067811865487940, -0.7071067811865463515, 0.000000000000000000 ) ) ;
#24591=VECTOR ( 'NONE', #124516, 1000.000000000000000 ) ;
#24592=ORIENTED_EDGE ( 'NONE', *, *, #117460, .F. ) ;
#24593=EDGE_CURVE ( 'NONE', #82088, #48470, #91710, .T. ) ;
#24594=DIRECTION ( 'NONE',  ( -0.3543493200069162685, -0.000000000000000000, -0.9351131265310288487 ) ) ;
#24595=DIRECTION ( 'NONE',  ( -0.6830127018922180770, -0.6830127018922204085, -0.2588190451025213501 ) ) ;
#24596=ORIENTED_EDGE ( 'NONE', *, *, #1175, .T. ) ;
#24597=DIRECTION ( 'NONE',  ( -0.000000000000000000, -0.3543493200069152693, 0.9351131265310292928 ) ) ;
#24599=ORIENTED_EDGE ( 'NONE', *, *, #51089, .T. ) ;
#24600=VECTOR ( 'NONE', #90848, 1000.000000000000000 ) ;
#24602=DIRECTION ( 'NONE',  ( 0.7071067811865487940, 0.7071067811865463515, 0.000000000000000000 ) ) ;
#24604=VECTOR ( 'NONE', #23965, 999.9999999999998863 ) ;
#24605=FACE_OUTER_BOUND ( 'NONE', #112233, .T. ) ;
#24606=CARTESIAN_POINT ( 'NONE',  ( -14.99999999999989875, 12.83542986846996214, -1.025386466790335183 ) ) ;
#24607=DIRECTION ( 'NONE',  ( 0.000000000000000000, 1.000000000000000000, 0.000000000000000000 ) ) ;
#24608=LINE ( 'NONE', #22442, #44547 ) ;
#24609=EDGE_CURVE ( 'NONE', #7076, #110736, #70011, .T. ) ;
#24610=DIRECTION ( 'NONE',  ( 0.6830127018922180770, -0.6830127018922204085, -0.2588190451025213501 ) ) ;
#24614=DIRECTION ( 'NONE',  ( -0.000000000000000000, 0.000000000000000000, 1.000000000000000000 ) ) ;
#24615=AXIS2_PLACEMENT_3D ( 'NONE', #65303, #89866, #31233 ) ;
#24617=DIRECTION ( 'NONE',  ( -0.000000000000000000, 0.000000000000000000, 1.000000000000000000 ) ) ;
#24618=ORIENTED_EDGE ( 'NONE', *, *, #44709, .T. ) ;
#24621=VERTEX_POINT ( 'NONE', #3937 ) ;
#24622=ORIENTED_EDGE ( 'NONE', *, *, #51399, .F. ) ;
#24625=DIRECTION ( 'NONE',  ( 0.7071067811865486830, -0.7071067811865464625, -0.000000000000000000 ) ) ;
#24628=ORIENTED_EDGE ( 'NONE', *, *, #122970, .F. ) ;
#24629=CARTESIAN_POINT ( 'NONE',  ( -34.49999999999975842, -19.91253812416055879, 4.000000000000000000 ) ) ;
#24630=DIRECTION ( 'NONE',  ( -0.000000000000000000, 0.000000000000000000, 1.000000000000000000 ) ) ;
#24631=DIRECTION ( 'NONE',  ( -0.7071067811865486830, -0.7071067811865464625, 0.000000000000000000 ) ) ;
#24633=ADVANCED_FACE ( 'NONE', ( #81586 ), #125789, .F. ) ;
#24636=CARTESIAN_POINT ( 'NONE',  ( 7.499999999999961808, -20.94781430457061333, 5.000000000000000000 ) ) ;
#24637=CARTESIAN_POINT ( 'NONE',  ( 0.000000000000000000, 0.000000000000000000, 5.000000000000000000 ) ) ;
#24639=DIRECTION ( 'NONE',  ( -0.7071067811865486830, -0.7071067811865464625, -0.000000000000000000 ) ) ;
#24640=CARTESIAN_POINT ( 'NONE',  ( 18.06011071044008887, -9.740707523384184441, 10.89222023123376637 ) ) ;
#24642=VERTEX_POINT ( 'NONE', #79470 ) ;
#24643=ORIENTED_EDGE ( 'NONE', *, *, #11504, .F. ) ;
#24646=VERTEX_POINT ( 'NONE', #67871 ) ;
#24647=EDGE_CURVE ( 'NONE', #142592, #47990, #46101, .T. ) ;
#24651=EDGE_CURVE ( 'NONE', #101509, #63240, #89572, .T. ) ;
#24652=CARTESIAN_POINT ( 'NONE',  ( -26.16347128873434258, 15.75929247661555443, 9.299976744542860274 ) ) ;
#24653=FACE_OUTER_BOUND ( 'NONE', #128890, .T. ) ;
#24655=ORIENTED_EDGE ( 'NONE', *, *, #10182, .F. ) ;
#24656=ORIENTED_EDGE ( 'NONE', *, *, #59710, .F. ) ;
#24658=VECTOR ( 'NONE', #76524, 1000.000000000000000 ) ;
#24659=EDGE_CURVE ( 'NONE', #41224, #6884, #46845, .T. ) ;
#24660=FACE_OUTER_BOUND ( 'NONE', #103978, .T. ) ;
#24661=VERTEX_POINT ( 'NONE', #13413 ) ;
#24662=VERTEX_POINT ( 'NONE', #91032 ) ;
#24664=LINE ( 'NONE', #113822, #127867 ) ;
#24666=VECTOR ( 'NONE', #88927, 1000.000000000000000 ) ;
#24669=ORIENTED_EDGE ( 'NONE', *, *, #55004, .F. ) ;
#24672=ADVANCED_FACE ( 'NONE', ( #94550 ), #84439, .F. ) ;
#24673=LINE ( 'NONE', #59484, #15456 ) ;
#24676=EDGE_LOOP ( 'NONE', ( #63927, #137795, #19708, #93918 ) ) ;
#24679=CARTESIAN_POINT ( 'NONE',  ( 15.48921356237309510, -27.52281430457066236, 5.000000000000000000 ) ) ;
#24680=CARTESIAN_POINT ( 'NONE',  ( 0.000000000000000000, -21.72500000000000142, 0.000000000000000000 ) ) ;
#24683=CARTESIAN_POINT ( 'NONE',  ( 5.999999999999950262, -22.22500000000000853, 4.412002311790033104 ) ) ;
#24685=DIRECTION ( 'NONE',  ( -0.7071067811865486830, -0.7071067811865464625, 0.000000000000000000 ) ) ;
#24686=ADVANCED_FACE ( 'NONE', ( #82291 ), #38766, .F. ) ;
#24688=AXIS2_PLACEMENT_3D ( 'NONE', #51798, #121308, #75682 ) ;
#24689=FACE_BOUND ( 'NONE', #21002, .T. ) ;
#24690=EDGE_CURVE ( 'NONE', #28705, #37784, #4636, .T. ) ;
#24691=ORIENTED_EDGE ( 'NONE', *, *, #50913, .T. ) ;
#24694=DIRECTION ( 'NONE',  ( 1.000000000000000000, 0.000000000000000000, 0.000000000000000000 ) ) ;
#24695=ADVANCED_FACE ( 'NONE', ( #103987 ), #17697, .F. ) ;
#24696=ORIENTED_EDGE ( 'NONE', *, *, #80401, .T. ) ;
#24697=LINE ( 'NONE', #4301, #18040 ) ;
#24698=ORIENTED_EDGE ( 'NONE', *, *, #33045, .F. ) ;
#24700=VECTOR ( 'NONE', #54139, 999.9999999999998863 ) ;
#24701=ORIENTED_EDGE ( 'NONE', *, *, #5743, .F. ) ;
#24702=VECTOR ( 'NONE', #96498, 1000.000000000000000 ) ;
#24703=VECTOR ( 'NONE', #72304, 1000.000000000000000 ) ;
#24705=EDGE_CURVE ( 'NONE', #129502, #4418, #61968, .T. ) ;
#24707=EDGE_CURVE ( 'NONE', #109252, #62370, #114861, .T. ) ;
#24710=ORIENTED_EDGE ( 'NONE', *, *, #137724, .T. ) ;
#24712=CARTESIAN_POINT ( 'NONE',  ( -31.17183060077625356, 21.75929247661549581, 4.000000000000000000 ) ) ;
#24713=AXIS2_PLACEMENT_3D ( 'NONE', #44074, #36748, #57824 ) ;
#24714=EDGE_CURVE ( 'NONE', #73986, #13719, #117434, .T. ) ;
#24716=CARTESIAN_POINT ( 'NONE',  ( 30.70710678118632941, -18.74070752338409207, 5.000000000000000000 ) ) ;
#24717=DIRECTION ( 'NONE',  ( -0.7071067811865487940, 0.7071067811865463515, -0.000000000000000000 ) ) ;
#24718=DIRECTION ( 'NONE',  ( -0.7071067811865486830, -0.7071067811865464625, 0.000000000000000000 ) ) ;
#24719=VERTEX_POINT ( 'NONE', #39496 ) ;
#24720=VERTEX_POINT ( 'NONE', #18401 ) ;
#24721=ADVANCED_FACE ( 'NONE', ( #83730 ), #73547, .F. ) ;
#24722=ORIENTED_EDGE ( 'NONE', *, *, #2904, .T. ) ;
#24723=ORIENTED_EDGE ( 'NONE', *, *, #104739, .T. ) ;
#24724=CARTESIAN_POINT ( 'NONE',  ( 21.62762920772360786, 8.558752285115851066, 4.000000000000000000 ) ) ;
#24725=VERTEX_POINT ( 'NONE', #51801 ) ;
#24726=ORIENTED_EDGE ( 'NONE', *, *, #30605, .F. ) ;
#24728=CARTESIAN_POINT ( 'NONE',  ( 34.82816939922328459, 12.75929247661558996, 4.000000000000000000 ) ) ;
#24729=EDGE_LOOP ( 'NONE', ( #4254, #138901, #38874, #65835 ) ) ;
#24730=VECTOR ( 'NONE', #58494, 1000.000000000000000 ) ;
#24731=ADVANCED_FACE ( 'NONE', ( #27879 ), #95985, .F. ) ;
#24732=PLANE ( 'NONE',  #60383 ) ;
#24733=VERTEX_POINT ( 'NONE', #60553 ) ;
#24735=EDGE_CURVE ( 'NONE', #68652, #2255, #40911, .T. ) ;
#24737=VECTOR ( 'NONE', #27874, 1000.000000000000000 ) ;
#24738=PLANE ( 'NONE',  #92393 ) ;
#24739=ORIENTED_EDGE ( 'NONE', *, *, #57916, .T. ) ;
#24741=CARTESIAN_POINT ( 'NONE',  ( 9.792893218813391698, 15.75929247661555976, 5.000000000000000000 ) ) ;
#24742=( BOUNDED_CURVE ( )  B_SPLINE_CURVE ( 3, ( #83747, #29316, #136651, #4657 ),
 .UNSPECIFIED., .F., .T. ) 
 B_SPLINE_CURVE_WITH_KNOTS ( ( 4, 4 ),
 ( 1.901594255663616728, 1.933014472006574280 ),
 .UNSPECIFIED. ) 
 CURVE ( )  GEOMETRIC_REPRESENTATION_ITEM ( )  RATIONAL_B_SPLINE_CURVE ( ( 1.000000000000000000, 0.9999177325257867510, 0.9999177325257867510, 1.000000000000000000 ) ) 
 REPRESENTATION_ITEM ( '' )  );
#24743=DIRECTION ( 'NONE',  ( 0.6830127018922181881, 0.6830127018922202975, -0.2588190451025214056 ) ) ;
#24744=CARTESIAN_POINT ( 'NONE',  ( -22.49999999999984368, 21.43112307739195899, 4.000000000000000000 ) ) ;
#24745=ORIENTED_EDGE ( 'NONE', *, *, #21542, .F. ) ;
#24746=LINE ( 'NONE', #43648, #26384 ) ;
#24747=CARTESIAN_POINT ( 'NONE',  ( -23.99451991528749062, 28.92564299267954908, 4.000000000000000000 ) ) ;
#24748=EDGE_LOOP ( 'NONE', ( #44816, #77947, #87247, #10735, #10628, #2405 ) ) ;
#24750=DIRECTION ( 'NONE',  ( 1.000000000000000000, 0.000000000000000000, 0.000000000000000000 ) ) ;
#24752=FACE_OUTER_BOUND ( 'NONE', #138791, .T. ) ;
#24753=LINE ( 'NONE', #35680, #135661 ) ;
#24754=ADVANCED_FACE ( 'NONE', ( #28623 ), #129325, .T. ) ;
#24755=CARTESIAN_POINT ( 'NONE',  ( -24.18398860626899705, 28.73617430169804265, 5.000000000000000000 ) ) ;
#24758=LINE ( 'NONE', #112489, #122354 ) ;
#24759=LINE ( 'NONE', #111025, #27999 ) ;
#24760=CYLINDRICAL_SURFACE ( 'NONE', #118492, 5.968999999999998529 ) ;
#24761=VECTOR ( 'NONE', #121079, 1000.000000000000000 ) ;
#24762=ORIENTED_EDGE ( 'NONE', *, *, #74947, .T. ) ;
#24763=CARTESIAN_POINT ( 'NONE',  ( 14.99999999999989875, 2.342191155542461267, -5.001666872980119471 ) ) ;
#24764=ORIENTED_EDGE ( 'NONE', *, *, #20831, .T. ) ;
#24765=VECTOR ( 'NONE', #117379, 1000.000000000000000 ) ;
#24766=LINE ( 'NONE', #93604, #37101 ) ;
#24767=ORIENTED_EDGE ( 'NONE', *, *, #72494, .F. ) ;
#24768=EDGE_LOOP ( 'NONE', ( #53099, #116561, #25080 ) ) ;
#24770=CARTESIAN_POINT ( 'NONE',  ( 30.79289321881324781, 9.759292476615627265, 5.000000000000000000 ) ) ;
#24771=ORIENTED_EDGE ( 'NONE', *, *, #15946, .T. ) ;
#24772=VECTOR ( 'NONE', #114569, 999.9999999999998863 ) ;
#24773=CARTESIAN_POINT ( 'NONE',  ( 12.18398860626900060, 28.73617430169795739, 5.000000000000000000 ) ) ;
#24775=CARTESIAN_POINT ( 'NONE',  ( -24.12147316337132352, -20.24070752338407786, 7.412974875817845977 ) ) ;
#24777=DIRECTION ( 'NONE',  ( 0.3543493200069162685, -0.000000000000000000, -0.9351131265310288487 ) ) ;
#24779=CARTESIAN_POINT ( 'NONE',  ( 36.48921356237310221, -27.52281430457080802, 5.000000000000000000 ) ) ;
#24781=DIRECTION ( 'NONE',  ( 0.3543493200069162685, -0.000000000000000000, -0.9351131265310288487 ) ) ;
#24782=ORIENTED_EDGE ( 'NONE', *, *, #74786, .T. ) ;
#24783=EDGE_LOOP ( 'NONE', ( #122449, #74990, #58078, #111229 ) ) ;
#24784=EDGE_LOOP ( 'NONE', ( #1330, #54795, #91454, #104250 ) ) ;
#24787=ORIENTED_EDGE ( 'NONE', *, *, #113327, .F. ) ;
#24788=ORIENTED_EDGE ( 'NONE', *, *, #97316, .F. ) ;
#24791=CARTESIAN_POINT ( 'NONE',  ( -60.29974487139158867, -27.71228299555248142, 4.000000000000000000 ) ) ;
#24792=EDGE_LOOP ( 'NONE', ( #39357, #33755, #123387, #72207 ) ) ;
#24793=DIRECTION ( 'NONE',  ( -0.000000000000000000, 0.3543493200069153248, 0.9351131265310292928 ) ) ;
#24794=CARTESIAN_POINT ( 'NONE',  ( 18.70710678118641468, -9.740707523384177335, 5.000000000000000000 ) ) ;
#24795=EDGE_CURVE ( 'NONE', #110391, #43579, #10397, .T. ) ;
#24796=FACE_OUTER_BOUND ( 'NONE', #81252, .T. ) ;
#24797=VECTOR ( 'NONE', #111879, 1000.000000000000000 ) ;
#24798=LINE ( 'NONE', #2301, #83568 ) ;
#24800=ADVANCED_FACE ( 'NONE', ( #209 ), #32916, .F. ) ;
#24801=ORIENTED_EDGE ( 'NONE', *, *, #79162, .F. ) ;
#24802=LINE ( 'NONE', #12493, #69659 ) ;
#24803=CARTESIAN_POINT ( 'NONE',  ( -51.48921356237309510, -27.52281430457091460, 5.000000000000000000 ) ) ;
#24804=CARTESIAN_POINT ( 'NONE',  ( 6.183988606268994381, 28.73617430169791476, 5.000000000000000000 ) ) ;
#24805=LINE ( 'NONE', #102402, #71391 ) ;
#24806=LINE ( 'NONE', #115346, #82257 ) ;
#24807=EDGE_CURVE ( 'NONE', #107783, #2199, #110416, .T. ) ;
#24808=AXIS2_PLACEMENT_3D ( 'NONE', #41620, #108264, #53961 ) ;
#24809=DIRECTION ( 'NONE',  ( -0.7071067811865486830, -0.7071067811865464625, 0.000000000000000000 ) ) ;
#24811=VECTOR ( 'NONE', #120958, 1000.000000000000227 ) ;
#24812=EDGE_CURVE ( 'NONE', #57387, #136867, #118449, .T. ) ;
#24814=ADVANCED_FACE ( 'NONE', ( #43069 ), #108988, .F. ) ;
#24815=LINE ( 'NONE', #66901, #120837 ) ;
#24816=VECTOR ( 'NONE', #10199, 999.9999999999998863 ) ;
#24817=CARTESIAN_POINT ( 'NONE',  ( 15.48921356237309510, -27.52281430457066236, 5.000000000000000000 ) ) ;
#24818=ORIENTED_EDGE ( 'NONE', *, *, #46441, .F. ) ;
#24819=ORIENTED_EDGE ( 'NONE', *, *, #54793, .T. ) ;
#24821=VERTEX_POINT ( 'NONE', #99542 ) ;
#24822=ADVANCED_FACE ( 'NONE', ( #142376 ), #11092, .F. ) ;
#24823=CARTESIAN_POINT ( 'NONE',  ( 11.51078643762690490, -27.52281430457047406, 5.000000000000000000 ) ) ;
#24824=AXIS2_PLACEMENT_3D ( 'NONE', #102040, #89728, #47006 ) ;
#24825=VECTOR ( 'NONE', #61942, 1000.000000000000227 ) ;
#24828=LINE ( 'NONE', #111093, #46888 ) ;
#24829=ADVANCED_FACE ( 'NONE', ( #131489 ), #140913, .F. ) ;
#24831=ORIENTED_EDGE ( 'NONE', *, *, #76517, .F. ) ;
#24832=DIRECTION ( 'NONE',  ( 2.781805975412905890E-17, -0.3543493200069152693, 0.9351131265310292928 ) ) ;
#24833=VERTEX_POINT ( 'NONE', #120567 ) ;
#24834=CARTESIAN_POINT ( 'NONE',  ( 8.999999999999934275, 19.55218569542897100, 5.000000000000000000 ) ) ;
#24837=DIRECTION ( 'NONE',  ( -0.6830127018922180770, -0.6830127018922204085, -0.2588190451025213501 ) ) ;
#24838=DIRECTION ( 'NONE',  ( 0.6830127018922180770, -0.6830127018922204085, -0.2588190451025213501 ) ) ;
#24839=EDGE_LOOP ( 'NONE', ( #52875, #93709, #109898, #83200 ) ) ;
#24840=PLANE ( 'NONE',  #23352 ) ;
#24841=ORIENTED_EDGE ( 'NONE', *, *, #27571, .F. ) ;
#24843=LINE ( 'NONE', #1625, #2222 ) ;
#24844=DIRECTION ( 'NONE',  ( 0.3543493200069162685, -0.000000000000000000, -0.9351131265310288487 ) ) ;
#24846=ADVANCED_FACE ( 'NONE', ( #64812 ), #53194, .F. ) ;
#24847=CARTESIAN_POINT ( 'NONE',  ( 57.29974487139158157, -27.71228299555246011, 4.000000000000000000 ) ) ;
#24848=CARTESIAN_POINT ( 'NONE',  ( -30.12147316337128800, -20.24070752338407431, 7.412974875817861076 ) ) ;
#24849=VECTOR ( 'NONE', #75255, 1000.000000000000000 ) ;
#24850=LINE ( 'NONE', #84088, #87091 ) ;
#24852=LINE ( 'NONE', #122005, #9305 ) ;
#24853=ADVANCED_FACE ( 'NONE', ( #130063 ), #21297, .F. ) ;
#24854=LINE ( 'NONE', #69098, #38688 ) ;
#24855=ORIENTED_EDGE ( 'NONE', *, *, #70977, .T. ) ;
#24856=ORIENTED_EDGE ( 'NONE', *, *, #118944, .T. ) ;
#24857=CARTESIAN_POINT ( 'NONE',  ( 15.85005128541015118, -8.240707523384193323, 17.25253755692242663 ) ) ;
#24859=EDGE_CURVE ( 'NONE', #71177, #59824, #43762, .T. ) ;
#24860=EDGE_CURVE ( 'NONE', #125463, #35816, #63411, .T. ) ;
#24861=CARTESIAN_POINT ( 'NONE',  ( -63.18398860626900415, 28.73617430169831621, 5.000000000000000000 ) ) ;
#24862=ORIENTED_EDGE ( 'NONE', *, *, #37969, .T. ) ;
#24865=EDGE_CURVE ( 'NONE', #65337, #23121, #64547, .T. ) ;
#24866=FACE_OUTER_BOUND ( 'NONE', #38042, .T. ) ;
#24867=FACE_BOUND ( 'NONE', #60484, .T. ) ;
#24868=EDGE_CURVE ( 'NONE', #97631, #28308, #119167, .T. ) ;
#24870=CARTESIAN_POINT ( 'NONE',  ( 0.000000000000000000, 0.000000000000000000, 5.000000000000000000 ) ) ;
#24871=DIRECTION ( 'NONE',  ( -0.7071067811865486830, -0.7071067811865464625, 0.000000000000000000 ) ) ;
#24872=ORIENTED_EDGE ( 'NONE', *, *, #117840, .T. ) ;
#24874=DIRECTION ( 'NONE',  ( -0.000000000000000000, 0.000000000000000000, 1.000000000000000000 ) ) ;
#24875=EDGE_LOOP ( 'NONE', ( #63111, #78593, #113323, #10872, #54122 ) ) ;
#24876=ORIENTED_EDGE ( 'NONE', *, *, #15736, .T. ) ;
#24878=ORIENTED_EDGE ( 'NONE', *, *, #119415, .T. ) ;
#24880=ADVANCED_FACE ( 'NONE', ( #1642 ), #89406, .T. ) ;
#24881=FACE_OUTER_BOUND ( 'NONE', #10172, .T. ) ;
#24882=VERTEX_POINT ( 'NONE', #14701 ) ;
#24884=ADVANCED_FACE ( 'NONE', ( #11814 ), #111881, .F. ) ;
#24885=DIRECTION ( 'NONE',  ( 0.6830127018922181881, 0.6830127018922202975, -0.2588190451025214056 ) ) ;
#24886=DIRECTION ( 'NONE',  ( -0.7071067811865486830, -0.7071067811865464625, 0.000000000000000000 ) ) ;
#24888=DIRECTION ( 'NONE',  ( -0.7071067811865487940, 0.7071067811865463515, -0.000000000000000000 ) ) ;
#24889=DIRECTION ( 'NONE',  ( -0.3543493200069162685, -0.000000000000000000, -0.9351131265310288487 ) ) ;
#24890=ORIENTED_EDGE ( 'NONE', *, *, #20739, .T. ) ;
#24891=ORIENTED_EDGE ( 'NONE', *, *, #105358, .F. ) ;
#24892=DIRECTION ( 'NONE',  ( -2.781805975412905890E-17, 0.3543493200069152693, 0.9351131265310292928 ) ) ;
#24894=DIRECTION ( 'NONE',  ( -0.7071067811865486830, 0.7071067811865464625, 0.000000000000000000 ) ) ;
#24895=ORIENTED_EDGE ( 'NONE', *, *, #121383, .T. ) ;
#24896=VERTEX_POINT ( 'NONE', #35780 ) ;
#24897=VECTOR ( 'NONE', #16273, 1000.000000000000000 ) ;
#24898=EDGE_LOOP ( 'NONE', ( #122667, #93359, #83336, #2161 ) ) ;
#24900=EDGE_LOOP ( 'NONE', ( #100331, #45757, #104997, #109498 ) ) ;
#24901=LINE ( 'NONE', #32971, #141265 ) ;
#24902=VECTOR ( 'NONE', #39894, 1000.000000000000000 ) ;
#24903=AXIS2_PLACEMENT_3D ( 'NONE', #138650, #14716, #27727 ) ;
#24904=EDGE_CURVE ( 'NONE', #115656, #127118, #56101, .T. ) ;
#24905=VECTOR ( 'NONE', #117871, 1000.000000000000000 ) ;
#24907=LINE ( 'NONE', #14017, #10156 ) ;
#24909=LINE ( 'NONE', #134412, #68955 ) ;
#24912=PLANE ( 'NONE',  #91478 ) ;
#24913=DIRECTION ( 'NONE',  ( -0.000000000000000000, -0.3543493200069152693, 0.9351131265310292928 ) ) ;
#24914=VERTEX_POINT ( 'NONE', #13959 ) ;
#24915=EDGE_LOOP ( 'NONE', ( #134550, #8420, #63874, #102184 ) ) ;
#24916=PLANE ( 'NONE',  #93542 ) ;
#24917=LINE ( 'NONE', #126372, #37623 ) ;
#24918=CARTESIAN_POINT ( 'NONE',  ( 10.49999999999993250, 3.073033219394637250, -6.593910359670946519 ) ) ;
#24919=ORIENTED_EDGE ( 'NONE', *, *, #24367, .F. ) ;
#24920=PLANE ( 'NONE',  #3897 ) ;
#24922=PLANE ( 'NONE',  #100394 ) ;
#24923=ORIENTED_EDGE ( 'NONE', *, *, #11600, .T. ) ;
#24924=DIRECTION ( 'NONE',  ( 4.681814790819592407E-17, 0.3543493200069153248, 0.9351131265310292928 ) ) ;
#24926=FACE_OUTER_BOUND ( 'NONE', #105562, .T. ) ;
#24927=CARTESIAN_POINT ( 'NONE',  ( -42.48921356237308800, -27.52281430457085065, 5.000000000000000000 ) ) ;
#24928=DIRECTION ( 'NONE',  ( -0.3543493200069162685, -0.000000000000000000, -0.9351131265310288487 ) ) ;
#24929=ORIENTED_EDGE ( 'NONE', *, *, #27127, .F. ) ;
#24930=ORIENTED_EDGE ( 'NONE', *, *, #99993, .T. ) ;
#24932=FACE_OUTER_BOUND ( 'NONE', #29897, .T. ) ;
#24935=CARTESIAN_POINT ( 'NONE',  ( 22.49999999999984723, -9.462702396500988655, -9.474982329943564707 ) ) ;
#24936=DIRECTION ( 'NONE',  ( 0.7071067811865487940, -0.7071067811865463515, 0.000000000000000000 ) ) ;
#24937=CARTESIAN_POINT ( 'NONE',  ( 16.17183060077636014, 15.75929247661555443, 4.000000000000000000 ) ) ;
#24938=ORIENTED_EDGE ( 'NONE', *, *, #107182, .F. ) ;
#24940=DIRECTION ( 'NONE',  ( -0.7071067811865486830, 0.7071067811865464625, 0.000000000000000000 ) ) ;
#24942=CARTESIAN_POINT ( 'NONE',  ( 54.18398860626899705, 28.73617430169825226, 5.000000000000000000 ) ) ;
#24944=LINE ( 'NONE', #135191, #100 ) ;
#24945=ORIENTED_EDGE ( 'NONE', *, *, #40546, .F. ) ;
#24946=CARTESIAN_POINT ( 'NONE',  ( 19.17183060077634593, 18.75929247661552779, 4.000000000000000000 ) ) ;
#24947=EDGE_LOOP ( 'NONE', ( #29701, #23112, #105287, #88007 ) ) ;
#24949=DIRECTION ( 'NONE',  ( -0.7071067811865486830, -0.7071067811865464625, 0.000000000000000000 ) ) ;
#24950=DIRECTION ( 'NONE',  ( -0.7071067811865487940, 0.7071067811865463515, 0.000000000000000000 ) ) ;
#24952=EDGE_CURVE ( 'NONE', #114916, #115494, #100294, .T. ) ;
#24953=DIRECTION ( 'NONE',  ( -0.7071067811865486830, -0.7071067811865464625, 0.000000000000000000 ) ) ;
#24954=DIRECTION ( 'NONE',  ( -0.6830127018922180770, -0.6830127018922204085, -0.2588190451025213501 ) ) ;
#24955=DIRECTION ( 'NONE',  ( 0.6830127018922181881, 0.6830127018922202975, -0.2588190451025214056 ) ) ;
#24956=EDGE_CURVE ( 'NONE', #20512, #122084, #112589, .T. ) ;
#24958=VERTEX_POINT ( 'NONE', #122010 ) ;
#24959=EDGE_LOOP ( 'NONE', ( #51243, #76106, #78357, #5440 ) ) ;
#24960=CARTESIAN_POINT ( 'NONE',  ( -6.299744871391586898, -27.71228299555210484, 4.000000000000000000 ) ) ;
#24961=DIRECTION ( 'NONE',  ( -0.7071067811865487940, 0.7071067811865463515, 0.000000000000000000 ) ) ;
#24963=FACE_OUTER_BOUND ( 'NONE', #32107, .T. ) ;
#24964=EDGE_CURVE ( 'NONE', #63769, #131639, #48059, .T. ) ;
#24966=ADVANCED_FACE ( 'NONE', ( #80688 ), #101703, .F. ) ;
#24967=DIRECTION ( 'NONE',  ( -0.7071067811865486830, -0.7071067811865464625, -0.000000000000000000 ) ) ;
#24968=DIRECTION ( 'NONE',  ( -0.7071067811865487940, 0.7071067811865463515, 0.000000000000000000 ) ) ;
#24969=ORIENTED_EDGE ( 'NONE', *, *, #141668, .T. ) ;
#24970=AXIS2_PLACEMENT_3D ( 'NONE', #142910, #87811, #10932 ) ;
#24974=CARTESIAN_POINT ( 'NONE',  ( -34.47516574401893052, -1.509482387884379939, 4.998110765256835286 ) ) ;
#24977=ORIENTED_EDGE ( 'NONE', *, *, #18314, .T. ) ;
#24978=LINE ( 'NONE', #26433, #18985 ) ;
#24979=EDGE_CURVE ( 'NONE', #78390, #4806, #67693, .T. ) ;
#24980=AXIS2_PLACEMENT_3D ( 'NONE', #142333, #76351, #120518 ) ;
#24981=CARTESIAN_POINT ( 'NONE',  ( 14.81601139373099585, 28.73617430169776910, 5.000000000000000000 ) ) ;
#24983=CARTESIAN_POINT ( 'NONE',  ( -34.49999999999976552, 13.46425560840034841, 4.994342998332165884 ) ) ;
#24985=ORIENTED_EDGE ( 'NONE', *, *, #18063, .F. ) ;
#24987=CARTESIAN_POINT ( 'NONE',  ( -78.48921356237309510, -27.52281430457109934, 5.000000000000000000 ) ) ;
#24988=EDGE_CURVE ( 'NONE', #8455, #111687, #134356, .T. ) ;
#24989=DIRECTION ( 'NONE',  ( -0.6830127018922181881, 0.6830127018922202975, -0.2588190451025214056 ) ) ;
#24990=VECTOR ( 'NONE', #11106, 1000.000000000000227 ) ;
#24991=DIRECTION ( 'NONE',  ( -0.000000000000000000, -0.3543493200069152693, 0.9351131265310292928 ) ) ;
#24992=CARTESIAN_POINT ( 'NONE',  ( -48.18398860626899705, 28.73617430169820608, 5.000000000000000000 ) ) ;
#24994=VERTEX_POINT ( 'NONE', #135093 ) ;
#24995=DIRECTION ( 'NONE',  ( 0.7071067811865487940, 0.7071067811865463515, 0.000000000000000000 ) ) ;
#24996=LINE ( 'NONE', #23584, #45350 ) ;
#24998=EDGE_CURVE ( 'NONE', #39797, #134968, #123498, .T. ) ;
#24999=VECTOR ( 'NONE', #15737, 1000.000000000000000 ) ;
#25000=DIRECTION ( 'NONE',  ( -0.7071067811865487940, 0.7071067811865463515, 0.000000000000000000 ) ) ;
#25001=AXIS2_PLACEMENT_3D ( 'NONE', #2773, #2020, #46332 ) ;
#25002=ORIENTED_EDGE ( 'NONE', *, *, #35830, .T. ) ;
#25003=ORIENTED_EDGE ( 'NONE', *, *, #3823, .T. ) ;
#25005=ORIENTED_EDGE ( 'NONE', *, *, #91434, .F. ) ;
#25006=PLANE ( 'NONE',  #40637 ) ;
#25007=LINE ( 'NONE', #110580, #98933 ) ;
#25008=LINE ( 'NONE', #22848, #133628 ) ;
#25009=EDGE_CURVE ( 'NONE', #8977, #98083, #77826, .T. ) ;
#25010=DIRECTION ( 'NONE',  ( 0.7071067811865487940, -0.7071067811865463515, 0.000000000000000000 ) ) ;
#25014=CARTESIAN_POINT ( 'NONE',  ( 45.18398860626900415, 28.73617430169818832, 5.000000000000000000 ) ) ;
#25016=EDGE_CURVE ( 'NONE', #108338, #86073, #26299, .T. ) ;
#25017=ORIENTED_EDGE ( 'NONE', *, *, #84533, .F. ) ;
#25018=ORIENTED_EDGE ( 'NONE', *, *, #36282, .T. ) ;
#25019=EDGE_CURVE ( 'NONE', #120738, #84062, #61123, .T. ) ;
#25021=CARTESIAN_POINT ( 'NONE',  ( -18.48921356237309510, -27.52281430457068367, 5.000000000000000000 ) ) ;
#25022=( BOUNDED_CURVE ( )  B_SPLINE_CURVE ( 3, ( #141529, #129935, #85692, #30640 ),
 .UNSPECIFIED., .F., .T. ) 
 B_SPLINE_CURVE_WITH_KNOTS ( ( 4, 4 ),
 ( 2.001653308786163876, 3.503810798801451742 ),
 .UNSPECIFIED. ) 
 CURVE ( )  GEOMETRIC_REPRESENTATION_ITEM ( )  RATIONAL_B_SPLINE_CURVE ( ( 1.000000000000000000, 0.8206354192515226131, 0.8206354192515226131, 1.000000000000000000 ) ) 
 REPRESENTATION_ITEM ( '' )  );
#25023=EDGE_CURVE ( 'NONE', #37506, #14791, #138633, .T. ) ;
#25024=ORIENTED_EDGE ( 'NONE', *, *, #143287, .T. ) ;
#25025=AXIS2_PLACEMENT_3D ( 'NONE', #135174, #123590, #14056 ) ;
#25026=EDGE_CURVE ( 'NONE', #35802, #126591, #116144, .T. ) ;
#25027=FACE_BOUND ( 'NONE', #10582, .T. ) ;
#25029=FACE_OUTER_BOUND ( 'NONE', #79229, .T. ) ;
#25030=DIRECTION ( 'NONE',  ( 1.000000000000000000, 0.000000000000000000, 0.000000000000000000 ) ) ;
#25031=AXIS2_PLACEMENT_3D ( 'NONE', #29006, #20241, #130475 ) ;
#25032=DIRECTION ( 'NONE',  ( 0.3543493200069162685, -0.000000000000000000, -0.9351131265310288487 ) ) ;
#25033=LINE ( 'NONE', #98167, #104176 ) ;
#25035=VERTEX_POINT ( 'NONE', #27707 ) ;
#25038=ORIENTED_EDGE ( 'NONE', *, *, #91759, .T. ) ;
#25039=ADVANCED_FACE ( 'NONE', ( #103812 ), #126314, .T. ) ;
#25040=CARTESIAN_POINT ( 'NONE',  ( -11.51078643762690490, -27.52281430457047406, 5.000000000000000000 ) ) ;
#25042=CARTESIAN_POINT ( 'NONE',  ( 14.99451991528749595, 28.92564299267948513, 4.000000000000000000 ) ) ;
#25043=VECTOR ( 'NONE', #131167, 1000.000000000000000 ) ;
#25044=DIRECTION ( 'NONE',  ( -0.000000000000000000, 0.3543493200069153248, 0.9351131265310292928 ) ) ;
#25045=AXIS2_PLACEMENT_3D ( 'NONE', #33725, #109829, #67050 ) ;
#25046=CARTESIAN_POINT ( 'NONE',  ( 4.499999999999962697, -1.592773361805368992, -6.492772025301240646 ) ) ;
#25047=VERTEX_POINT ( 'NONE', #114703 ) ;
#25048=CARTESIAN_POINT ( 'NONE',  ( 10.49999999999992539, 13.56627193232215767, -10.57019076586066397 ) ) ;
#25049=FACE_OUTER_BOUND ( 'NONE', #120188, .T. ) ;
#25052=LINE ( 'NONE', #135290, #36889 ) ;
#25053=DIRECTION ( 'NONE',  ( -0.000000000000000000, -0.3543493200069152693, 0.9351131265310292928 ) ) ;
#25055=CARTESIAN_POINT ( 'NONE',  ( -11.99999999999991651, -13.06887692260767686, 4.000000000000000000 ) ) ;
#25056=CARTESIAN_POINT ( 'NONE',  ( 18.48921356237309510, -27.52281430457068367, 5.000000000000000000 ) ) ;
#25057=ORIENTED_EDGE ( 'NONE', *, *, #134251, .F. ) ;
#25058=EDGE_CURVE ( 'NONE', #31872, #104365, #5924, .T. ) ;
#25059=VERTEX_POINT ( 'NONE', #82833 ) ;
#25060=VERTEX_POINT ( 'NONE', #50908 ) ;
#25062=ORIENTED_EDGE ( 'NONE', *, *, #63698, .T. ) ;
#25064=VECTOR ( 'NONE', #22712, 1000.000000000000227 ) ;
#25066=LINE ( 'NONE', #123714, #56480 ) ;
#25067=EDGE_LOOP ( 'NONE', ( #86892, #114399, #64679, #38504 ) ) ;
#25068=CARTESIAN_POINT ( 'NONE',  ( 30.48921356237309510, -27.52281430457076894, 5.000000000000000000 ) ) ;
#25069=ORIENTED_EDGE ( 'NONE', *, *, #94390, .F. ) ;
#25070=DIRECTION ( 'NONE',  ( 0.7071067811865487940, 0.7071067811865463515, 0.000000000000000000 ) ) ;
#25071=CARTESIAN_POINT ( 'NONE',  ( 25.82816939922334853, 9.759292476615621936, 4.000000000000000000 ) ) ;
#25072=VERTEX_POINT ( 'NONE', #71244 ) ;
#25073=EDGE_CURVE ( 'NONE', #86413, #91617, #137921, .T. ) ;
#25075=FACE_OUTER_BOUND ( 'NONE', #37120, .T. ) ;
#25076=DIRECTION ( 'NONE',  ( 0.7071067811865486830, -0.7071067811865464625, -0.000000000000000000 ) ) ;
#25077=VERTEX_POINT ( 'NONE', #115389 ) ;
#25078=EDGE_CURVE ( 'NONE', #30236, #74065, #60377, .T. ) ;
#25079=VECTOR ( 'NONE', #3680, 999.9999999999998863 ) ;
#25080=ORIENTED_EDGE ( 'NONE', *, *, #63935, .T. ) ;
#25081=VERTEX_POINT ( 'NONE', #94388 ) ;
#25083=DIRECTION ( 'NONE',  ( -0.7071067811865486830, -0.7071067811865464625, 0.000000000000000000 ) ) ;
#25084=VECTOR ( 'NONE', #63063, 1000.000000000000114 ) ;
#25085=VECTOR ( 'NONE', #54386, 1000.000000000000000 ) ;
#25086=CARTESIAN_POINT ( 'NONE',  ( 4.171830600776445408, -8.240707523384198652, 4.000000000000000000 ) ) ;
#25087=VECTOR ( 'NONE', #46113, 1000.000000000000227 ) ;
#25088=CARTESIAN_POINT ( 'NONE',  ( 3.489213562373097322, -27.52281430457057709, 5.000000000000000000 ) ) ;
#25089=DIRECTION ( 'NONE',  ( 0.3543493200069162685, -0.000000000000000000, -0.9351131265310288487 ) ) ;
#25090=EDGE_CURVE ( 'NONE', #3994, #137018, #134973, .T. ) ;
#25091=VECTOR ( 'NONE', #67210, 999.9999999999998863 ) ;
#25093=VERTEX_POINT ( 'NONE', #83550 ) ;
#25095=VECTOR ( 'NONE', #103909, 999.9999999999998863 ) ;
#25096=DIRECTION ( 'NONE',  ( 0.7071067811865487940, 0.7071067811865463515, -0.000000000000000000 ) ) ;
#25099=DIRECTION ( 'NONE',  ( -0.000000000000000000, -0.3543493200069152693, 0.9351131265310292928 ) ) ;
#25100=DIRECTION ( 'NONE',  ( 0.7071067811865487940, 0.7071067811865463515, 0.000000000000000000 ) ) ;
#25101=ORIENTED_EDGE ( 'NONE', *, *, #92101, .F. ) ;
#25106=VECTOR ( 'NONE', #101615, 1000.000000000000000 ) ;
#25107=LINE ( 'NONE', #71499, #56729 ) ;
#25108=CARTESIAN_POINT ( 'NONE',  ( 0.000000000000000000, 0.000000000000000000, 5.000000000000000000 ) ) ;
#25109=LINE ( 'NONE', #56380, #22301 ) ;
#25112=CARTESIAN_POINT ( 'NONE',  ( 42.29974487139158157, -27.71228299555235708, 4.000000000000000000 ) ) ;
#25113=PLANE ( 'NONE',  #106828 ) ;
#25114=CARTESIAN_POINT ( 'NONE',  ( -5.510786437626906675, -27.52281430457051314, 5.000000000000000000 ) ) ;
#25115=DIRECTION ( 'NONE',  ( 0.7071067811865487940, 0.7071067811865463515, 0.000000000000000000 ) ) ;
#25116=EDGE_LOOP ( 'NONE', ( #56668, #139399, #112357, #5395 ) ) ;
#25118=EDGE_CURVE ( 'NONE', #26316, #50236, #28446, .T. ) ;
#25120=ORIENTED_EDGE ( 'NONE', *, *, #120253, .T. ) ;
#25121=VECTOR ( 'NONE', #67606, 1000.000000000000000 ) ;
#25123=CARTESIAN_POINT ( 'NONE',  ( 2.671830600776446740, -21.74070752338405654, 4.000000000000000000 ) ) ;
#25124=DIRECTION ( 'NONE',  ( -1.000000000000000000, 4.083240884147117807E-14, 0.000000000000000000 ) ) ;
#25125=ORIENTED_EDGE ( 'NONE', *, *, #137968, .F. ) ;
#25127=DIRECTION ( 'NONE',  ( -0.3543493200069162685, -0.000000000000000000, -0.9351131265310288487 ) ) ;
#25128=ADVANCED_FACE ( 'NONE', ( #104556 ), #116863, .F. ) ;
#25129=ORIENTED_EDGE ( 'NONE', *, *, #108815, .F. ) ;
#25130=DIRECTION ( 'NONE',  ( -0.000000000000000000, -0.3543493200069152693, 0.9351131265310292928 ) ) ;
#25131=VERTEX_POINT ( 'NONE', #48770 ) ;
#25132=PLANE ( 'NONE',  #25814 ) ;
#25134=VECTOR ( 'NONE', #2851, 1000.000000000000000 ) ;
#25135=CARTESIAN_POINT ( 'NONE',  ( 11.99999999999992184, 7.552185695429091794, 5.000000000000000000 ) ) ;
#25136=EDGE_CURVE ( 'NONE', #5782, #20512, #139370, .T. ) ;
#25140=DIRECTION ( 'NONE',  ( 0.3543493200069162685, -0.000000000000000000, -0.9351131265310288487 ) ) ;
#25141=ORIENTED_EDGE ( 'NONE', *, *, #72034, .F. ) ;
#25142=EDGE_CURVE ( 'NONE', #112149, #46262, #66443, .T. ) ;
#25143=PLANE ( 'NONE',  #9831 ) ;
#25144=DIRECTION ( 'NONE',  ( 0.7071067811865487940, 0.7071067811865463515, 0.000000000000000000 ) ) ;
#25145=EDGE_CURVE ( 'NONE', #96120, #102869, #2566, .T. ) ;
#25146=LINE ( 'NONE', #36743, #13737 ) ;
#25149=VECTOR ( 'NONE', #135852, 1000.000000000000227 ) ;
#25150=CARTESIAN_POINT ( 'NONE',  ( 17.99451991528748351, 28.92564299267950645, 4.000000000000000000 ) ) ;
#25151=EDGE_CURVE ( 'NONE', #9218, #135984, #40087, .T. ) ;
#25152=VERTEX_POINT ( 'NONE', #33128 ) ;
#25153=AXIS2_PLACEMENT_3D ( 'NONE', #116253, #29233, #52409 ) ;
#25154=DIRECTION ( 'NONE',  ( 0.7071067811865487940, 0.7071067811865463515, 0.000000000000000000 ) ) ;
#25155=ADVANCED_FACE ( 'NONE', ( #101905 ), #78737, .F. ) ;
#25156=ORIENTED_EDGE ( 'NONE', *, *, #20587, .F. ) ;
#25158=PLANE ( 'NONE',  #22240 ) ;
#25159=DIRECTION ( 'NONE',  ( 0.7071067811865486830, -0.7071067811865464625, -0.000000000000000000 ) ) ;
#25160=FACE_OUTER_BOUND ( 'NONE', #1957, .T. ) ;
#25161=PLANE ( 'NONE',  #15460 ) ;
#25162=ORIENTED_EDGE ( 'NONE', *, *, #25985, .T. ) ;
#25163=CARTESIAN_POINT ( 'NONE',  ( 2.292986735706931345, -21.74070752338405654, 4.999753212805221558 ) ) ;
#25166=ORIENTED_EDGE ( 'NONE', *, *, #85, .T. ) ;
#25168=CARTESIAN_POINT ( 'NONE',  ( -34.92500000000001137, 22.22500000000000142, 4.000000000000000000 ) ) ;
#25169=DIRECTION ( 'NONE',  ( -0.7071067811865487940, 0.7071067811865463515, 0.000000000000000000 ) ) ;
#25171=EDGE_LOOP ( 'NONE', ( #22941, #122946, #96168, #131733 ) ) ;
#25172=LINE ( 'NONE', #69427, #136585 ) ;
#25174=DIRECTION ( 'NONE',  ( 0.3543493200069162685, -0.000000000000000000, -0.9351131265310288487 ) ) ;
#25175=DIRECTION ( 'NONE',  ( 0.7071067811865487940, 0.7071067811865463515, 0.000000000000000000 ) ) ;
#25176=ADVANCED_FACE ( 'NONE', ( #46873 ), #99757, .F. ) ;
#25177=CARTESIAN_POINT ( 'NONE',  ( -1.499999999999990008, 15.05218569542901186, 5.000000000000000000 ) ) ;
#25178=ORIENTED_EDGE ( 'NONE', *, *, #137923, .T. ) ;
#25179=ORIENTED_EDGE ( 'NONE', *, *, #83294, .F. ) ;
#25180=VERTEX_POINT ( 'NONE', #133827 ) ;
#25182=ORIENTED_EDGE ( 'NONE', *, *, #133464, .F. ) ;
#25185=DIRECTION ( 'NONE',  ( -0.6830127018922180770, -0.6830127018922204085, -0.2588190451025213501 ) ) ;
#25186=LINE ( 'NONE', #47017, #112567 ) ;
#25187=ORIENTED_EDGE ( 'NONE', *, *, #108086, .T. ) ;
#25190=CARTESIAN_POINT ( 'NONE',  ( -26.99999999999979394, 2.587461875839214720, 4.000000000000000000 ) ) ;
#25193=FACE_OUTER_BOUND ( 'NONE', #6787, .T. ) ;
#25194=ADVANCED_FACE ( 'NONE', ( #79498 ), #44725, .F. ) ;
#25195=DIRECTION ( 'NONE',  ( 0.000000000000000000, -0.3543493200069152138, 0.9351131265310292928 ) ) ;
#25196=CARTESIAN_POINT ( 'NONE',  ( 2.671830600776451181, -15.74070752338412760, 4.000000000000000000 ) ) ;
#25198=AXIS2_PLACEMENT_3D ( 'NONE', #130162, #43862, #141004 ) ;
#25199=VECTOR ( 'NONE', #49518, 1000.000000000000000 ) ;
#25200=EDGE_LOOP ( 'NONE', ( #125486, #2996, #136169, #125836 ) ) ;
#25201=ORIENTED_EDGE ( 'NONE', *, *, #45542, .F. ) ;
#25202=VECTOR ( 'NONE', #32557, 1000.000000000000000 ) ;
#25203=DIRECTION ( 'NONE',  ( 0.7071067811865487940, 0.7071067811865463515, 0.000000000000000000 ) ) ;
#25206=DIRECTION ( 'NONE',  ( 0.3543493200069162685, -0.000000000000000000, -0.9351131265310288487 ) ) ;
#25207=VECTOR ( 'NONE', #119548, 1000.000000000000000 ) ;
#25209=( BOUNDED_CURVE ( )  B_SPLINE_CURVE ( 3, ( #74025, #108037, #76169, #129101 ),
 .UNSPECIFIED., .F., .T. ) 
 B_SPLINE_CURVE_WITH_KNOTS ( ( 4, 4 ),
 ( 3.995629653766868294, 4.163580865291857336 ),
 .UNSPECIFIED. ) 
 CURVE ( )  GEOMETRIC_REPRESENTATION_ITEM ( )  RATIONAL_B_SPLINE_CURVE ( ( 1.000000000000000000, 0.9976507469244647597, 0.9976507469244647597, 1.000000000000000000 ) ) 
 REPRESENTATION_ITEM ( '' )  );
#25210=EDGE_CURVE ( 'NONE', #49508, #11167, #122209, .T. ) ;
#25211=CARTESIAN_POINT ( 'NONE',  ( 0.000000000000000000, 0.000000000000000000, 5.000000000000000000 ) ) ;
#25212=DIRECTION ( 'NONE',  ( -0.7071067811865487940, 0.7071067811865463515, 0.000000000000000000 ) ) ;
#25213=VERTEX_POINT ( 'NONE', #91060 ) ;
#25214=ORIENTED_EDGE ( 'NONE', *, *, #80067, .F. ) ;
#25216=EDGE_CURVE ( 'NONE', #28316, #48874, #99030, .T. ) ;
#25217=EDGE_LOOP ( 'NONE', ( #111195, #59292, #134518, #110623 ) ) ;
#25218=ORIENTED_EDGE ( 'NONE', *, *, #40487, .T. ) ;
#25222=VERTEX_POINT ( 'NONE', #45420 ) ;
#25223=CARTESIAN_POINT ( 'NONE',  ( 12.29974487139158512, -27.71228299555214747, 4.000000000000000000 ) ) ;
#25224=CARTESIAN_POINT ( 'NONE',  ( 10.49999999999992539, 4.466399257802213363, 5.000000000000000000 ) ) ;
#25225=EDGE_CURVE ( 'NONE', #95357, #99199, #143264, .T. ) ;
#25226=CARTESIAN_POINT ( 'NONE',  ( -8.999999999999937828, 12.25461709320620507, -10.07315571508699392 ) ) ;
#25228=LINE ( 'NONE', #81069, #81554 ) ;
#25229=ORIENTED_EDGE ( 'NONE', *, *, #620, .F. ) ;
#25230=VECTOR ( 'NONE', #74931, 1000.000000000000227 ) ;
#25231=DIRECTION ( 'NONE',  ( -0.6830127018922180770, -0.6830127018922204085, -0.2588190451025213501 ) ) ;
#25232=FACE_OUTER_BOUND ( 'NONE', #454, .T. ) ;
#25233=ORIENTED_EDGE ( 'NONE', *, *, #29375, .F. ) ;
#25234=CARTESIAN_POINT ( 'NONE',  ( 36.48921356237310221, -27.52281430457080802, 5.000000000000000000 ) ) ;
#25235=ADVANCED_FACE ( 'NONE', ( #77342 ), #88919, .T. ) ;
#25236=EDGE_LOOP ( 'NONE', ( #17195, #3429, #11412, #2916 ) ) ;
#25237=EDGE_LOOP ( 'NONE', ( #110238, #33276, #40216, #71620 ) ) ;
#25238=DIRECTION ( 'NONE',  ( -0.7071067811865486830, -0.7071067811865464625, -0.000000000000000000 ) ) ;
#25239=ORIENTED_EDGE ( 'NONE', *, *, #76703, .T. ) ;
#25240=EDGE_LOOP ( 'NONE', ( #119371, #65109, #15226, #85292 ) ) ;
#25243=EDGE_LOOP ( 'NONE', ( #114226, #4020, #78800, #69540 ) ) ;
#25244=VECTOR ( 'NONE', #73929, 1000.000000000000000 ) ;
#25245=CARTESIAN_POINT ( 'NONE',  ( 6.328169399223485314, -9.740707523384182664, 4.000000000000000000 ) ) ;
#25246=CARTESIAN_POINT ( 'NONE',  ( -36.48921356237310221, -27.52281430457080802, 5.000000000000000000 ) ) ;
#25247=DIRECTION ( 'NONE',  ( -0.6830127018922181881, 0.6830127018922202975, -0.2588190451025214056 ) ) ;
#25250=EDGE_CURVE ( 'NONE', #134254, #54031, #112086, .T. ) ;
#25252=CARTESIAN_POINT ( 'NONE',  ( 6.489213562373093325, -27.52281430457059841, 5.000000000000000000 ) ) ;
#25255=CARTESIAN_POINT ( 'NONE',  ( -21.48921356237309155, -27.52281430457070499, 5.000000000000000000 ) ) ;
#25256=DIRECTION ( 'NONE',  ( -0.7071067811865487940, 0.7071067811865463515, -0.000000000000000000 ) ) ;
#25257=VERTEX_POINT ( 'NONE', #425 ) ;
#25258=EDGE_CURVE ( 'NONE', #111297, #98615, #67147, .T. ) ;
#25259=DIRECTION ( 'NONE',  ( -0.000000000000000000, 0.000000000000000000, 1.000000000000000000 ) ) ;
#25260=DIRECTION ( 'NONE',  ( -0.000000000000000000, 0.000000000000000000, 1.000000000000000000 ) ) ;
#25262=ORIENTED_EDGE ( 'NONE', *, *, #131237, .F. ) ;
#25263=CARTESIAN_POINT ( 'NONE',  ( 27.29974487139158512, -27.71228299555225405, 4.000000000000000000 ) ) ;
#25264=ORIENTED_EDGE ( 'NONE', *, *, #40477, .T. ) ;
#25265=DIRECTION ( 'NONE',  ( 0.7071067811865487940, 0.7071067811865463515, 0.000000000000000000 ) ) ;
#25266=DIRECTION ( 'NONE',  ( 0.3543493200069163240, 0.000000000000000000, -0.9351131265310288487 ) ) ;
#25267=CARTESIAN_POINT ( 'NONE',  ( 7.566871997512529369, -21.74070752338406365, 6.915939825044055134 ) ) ;
#25268=ADVANCED_FACE ( 'NONE', ( #12023 ), #56312, .F. ) ;
#25269=DIRECTION ( 'NONE',  ( 0.7071067811865487940, 0.7071067811865463515, -0.000000000000000000 ) ) ;
#25270=ORIENTED_EDGE ( 'NONE', *, *, #18276, .T. ) ;
#25271=DIRECTION ( 'NONE',  ( -0.6830127018922181881, 0.6830127018922202975, -0.2588190451025214056 ) ) ;
#25272=ORIENTED_EDGE ( 'NONE', *, *, #138161, .F. ) ;
#25274=CARTESIAN_POINT ( 'NONE',  ( 29.99999999999979039, -15.03360074219758857, 5.000000000000000000 ) ) ;
#25276=EDGE_LOOP ( 'NONE', ( #26407, #65884, #6597, #77732 ) ) ;
#25277=DIRECTION ( 'NONE',  ( 0.7071067811865486830, -0.7071067811865464625, -0.000000000000000000 ) ) ;
#25278=LINE ( 'NONE', #3505, #14101 ) ;
#25279=EDGE_LOOP ( 'NONE', ( #9278, #1510, #21821, #115037 ) ) ;
#25280=EDGE_LOOP ( 'NONE', ( #75509, #67601, #83168 ) ) ;
#25281=VERTEX_POINT ( 'NONE', #38797 ) ;
#25283=DIRECTION ( 'NONE',  ( 0.3543493200069162685, -0.000000000000000000, -0.9351131265310288487 ) ) ;
#25284=CARTESIAN_POINT ( 'NONE',  ( 57.18398860626899705, 28.73617430169827358, 5.000000000000000000 ) ) ;
#25286=ORIENTED_EDGE ( 'NONE', *, *, #41528, .T. ) ;
#25287=CARTESIAN_POINT ( 'NONE',  ( -34.17183060077622514, 0.7592924766157138627, 4.000000000000000000 ) ) ;
#25288=DIRECTION ( 'NONE',  ( 0.000000000000000000, 0.000000000000000000, -1.000000000000000000 ) ) ;
#25289=CARTESIAN_POINT ( 'NONE',  ( -30.48921356237309510, -27.52281430457076894, 5.000000000000000000 ) ) ;
#25290=FACE_OUTER_BOUND ( 'NONE', #13023, .T. ) ;
#25291=ORIENTED_EDGE ( 'NONE', *, *, #74796, .F. ) ;
#25292=AXIS2_PLACEMENT_3D ( 'NONE', #111936, #101029, #24206 ) ;
#25293=VECTOR ( 'NONE', #38691, 1000.000000000000000 ) ;
#25294=VECTOR ( 'NONE', #18389, 1000.000000000000114 ) ;
#25295=DIRECTION ( 'NONE',  ( 0.7071067811865487940, 0.7071067811865463515, 0.000000000000000000 ) ) ;
#25296=ORIENTED_EDGE ( 'NONE', *, *, #51502, .T. ) ;
#25297=VECTOR ( 'NONE', #80363, 1000.000000000000227 ) ;
#25300=ORIENTED_EDGE ( 'NONE', *, *, #12405, .T. ) ;
#25301=DIRECTION ( 'NONE',  ( -0.3543493200069162685, -0.000000000000000000, -0.9351131265310288487 ) ) ;
#25302=PLANE ( 'NONE',  #115423 ) ;
#25303=ORIENTED_EDGE ( 'NONE', *, *, #48597, .F. ) ;
#25307=CARTESIAN_POINT ( 'NONE',  ( 10.49999999999993605, -7.420205493532887608, -2.617629953481229510 ) ) ;
#25308=ADVANCED_FACE ( 'NONE', ( #80885 ), #136665, .F. ) ;
#25309=CARTESIAN_POINT ( 'NONE',  ( 25.82816939922334853, -11.24070752338417201, 4.000000000000000000 ) ) ;
#25311=ADVANCED_FACE ( 'NONE', ( #47574 ), #4669, .F. ) ;
#25312=FACE_OUTER_BOUND ( 'NONE', #62899, .T. ) ;
#25313=PLANE ( 'NONE',  #100088 ) ;
#25314=LINE ( 'NONE', #112349, #118958 ) ;
#25315=EDGE_CURVE ( 'NONE', #23280, #97308, #70738, .T. ) ;
#25316=CARTESIAN_POINT ( 'NONE',  ( 23.20710678118638270, -20.24070752338408141, 5.000000000000000000 ) ) ;
#25318=CARTESIAN_POINT ( 'NONE',  ( -26.99999999999980815, 7.552185695429093570, 5.000000000000000000 ) ) ;
#25319=VECTOR ( 'NONE', #85763, 1000.000000000000000 ) ;
#25320=CARTESIAN_POINT ( 'NONE',  ( 27.29974487139158512, -27.71228299555225405, 4.000000000000000000 ) ) ;
#25323=FACE_OUTER_BOUND ( 'NONE', #133300, .T. ) ;
#25324=EDGE_CURVE ( 'NONE', #124072, #139654, #17044, .T. ) ;
#25325=ORIENTED_EDGE ( 'NONE', *, *, #41928, .F. ) ;
#25326=ORIENTED_EDGE ( 'NONE', *, *, #19109, .T. ) ;
#25328=ORIENTED_EDGE ( 'NONE', *, *, #100191, .F. ) ;
#25329=VERTEX_POINT ( 'NONE', #70038 ) ;
#25331=LINE ( 'NONE', #23172, #59563 ) ;
#25332=CARTESIAN_POINT ( 'NONE',  ( 28.77149322861317771, 20.25929247661551003, 7.808871592221835911 ) ) ;
#25334=ORIENTED_EDGE ( 'NONE', *, *, #12001, .T. ) ;
#25335=VECTOR ( 'NONE', #86385, 1000.000000000000000 ) ;
#25336=CARTESIAN_POINT ( 'NONE',  ( 14.66989781452726582, 17.25929247661554555, 19.83885114516067816 ) ) ;
#25337=VECTOR ( 'NONE', #14646, 1000.000000000000000 ) ;
#25339=EDGE_CURVE ( 'NONE', #124629, #102653, #135961, .T. ) ;
#25340=LINE ( 'NONE', #113790, #37112 ) ;
#25342=EDGE_CURVE ( 'NONE', #137290, #25946, #138832, .T. ) ;
#25344=FACE_OUTER_BOUND ( 'NONE', #10821, .T. ) ;
#25345=DIRECTION ( 'NONE',  ( -0.000000000000000000, -0.3543493200069152693, 0.9351131265310292928 ) ) ;
#25346=DIRECTION ( 'NONE',  ( 0.000000000000000000, 0.000000000000000000, -1.000000000000000000 ) ) ;
#25347=VECTOR ( 'NONE', #119821, 1000.000000000000227 ) ;
#25349=CARTESIAN_POINT ( 'NONE',  ( -45.48921356237309510, -27.52281430457087197, 5.000000000000000000 ) ) ;
#25350=CARTESIAN_POINT ( 'NONE',  ( 34.49999999999975131, 9.054329344830847504, 4.994342998332164107 ) ) ;
#25351=AXIS2_PLACEMENT_3D ( 'NONE', #142267, #8814, #130680 ) ;
#25352=DIRECTION ( 'NONE',  ( 0.6830127018922181881, 0.6830127018922202975, -0.2588190451025214056 ) ) ;
#25353=EDGE_CURVE ( 'NONE', #57316, #28471, #26491, .T. ) ;
#25354=CARTESIAN_POINT ( 'NONE',  ( -11.51078643762690490, -27.52281430457047406, 5.000000000000000000 ) ) ;
#25355=ORIENTED_EDGE ( 'NONE', *, *, #60001, .T. ) ;
#25358=VERTEX_POINT ( 'NONE', #50392 ) ;
#25359=CARTESIAN_POINT ( 'NONE',  ( -2.994519915287485734, 28.92564299267940342, 4.000000000000000000 ) ) ;
#25360=EDGE_CURVE ( 'NONE', #48528, #107040, #125816, .T. ) ;
#25361=AXIS2_PLACEMENT_3D ( 'NONE', #16958, #137320, #48884 ) ;
#25362=PLANE ( 'NONE',  #111552 ) ;
#25363=DIRECTION ( 'NONE',  ( -0.6830127018922180770, -0.6830127018922204085, -0.2588190451025213501 ) ) ;
#25365=ORIENTED_EDGE ( 'NONE', *, *, #85247, .T. ) ;
#25367=LINE ( 'NONE', #80497, #128679 ) ;
#25368=EDGE_CURVE ( 'NONE', #51437, #12698, #48237, .T. ) ;
#25369=ORIENTED_EDGE ( 'NONE', *, *, #60359, .F. ) ;
#25370=EDGE_LOOP ( 'NONE', ( #52717, #94324, #132502, #49727 ) ) ;
#25372=FACE_OUTER_BOUND ( 'NONE', #104898, .T. ) ;
#25375=EDGE_CURVE ( 'NONE', #5308, #117459, #36637, .T. ) ;
#25377=ORIENTED_EDGE ( 'NONE', *, *, #123106, .F. ) ;
#25378=DIRECTION ( 'NONE',  ( -0.000000000000000000, 0.000000000000000000, 1.000000000000000000 ) ) ;
#25379=ORIENTED_EDGE ( 'NONE', *, *, #13215, .F. ) ;
#25380=EDGE_LOOP ( 'NONE', ( #122405, #83824, #128634, #45254 ) ) ;
#25381=CARTESIAN_POINT ( 'NONE',  ( -15.79289321881334196, 15.75929247661555799, 5.000000000000000000 ) ) ;
#25382=CARTESIAN_POINT ( 'NONE',  ( -48.18398860626899705, 28.73617430169820608, 5.000000000000000000 ) ) ;
#25384=ORIENTED_EDGE ( 'NONE', *, *, #48230, .T. ) ;
#25385=PLANE ( 'NONE',  #94626 ) ;
#25387=DIRECTION ( 'NONE',  ( -0.7071067811865486830, -0.7071067811865463515, 0.000000000000000000 ) ) ;
#25388=VECTOR ( 'NONE', #119735, 1000.000000000000227 ) ;
#25389=VECTOR ( 'NONE', #90850, 1000.000000000000000 ) ;
#25391=AXIS2_PLACEMENT_3D ( 'NONE', #87309, #75030, #110452 ) ;
#25392=FACE_BOUND ( 'NONE', #55209, .T. ) ;
#25393=ORIENTED_EDGE ( 'NONE', *, *, #126470, .T. ) ;
#25395=DIRECTION ( 'NONE',  ( 1.000000000000000000, 0.000000000000000000, 0.000000000000000000 ) ) ;
#25396=DIRECTION ( 'NONE',  ( -0.7071067811865486830, -0.7071067811865464625, -0.000000000000000000 ) ) ;
#25397=ORIENTED_EDGE ( 'NONE', *, *, #126154, .T. ) ;
#25398=CARTESIAN_POINT ( 'NONE',  ( -34.45011844616455221, -16.48371918836235395, 5.000000000000000888 ) ) ;
#25399=VERTEX_POINT ( 'NONE', #82313 ) ;
#25400=ORIENTED_EDGE ( 'NONE', *, *, #99886, .T. ) ;
#25401=AXIS2_PLACEMENT_3D ( 'NONE', #60858, #115868, #115148 ) ;
#25402=VERTEX_POINT ( 'NONE', #15562 ) ;
#25404=ORIENTED_EDGE ( 'NONE', *, *, #56033, .F. ) ;
#25405=VECTOR ( 'NONE', #141181, 1000.000000000000000 ) ;
#25406=CARTESIAN_POINT ( 'NONE',  ( -14.51078643762690490, -27.52281430457045275, 5.000000000000000000 ) ) ;
#25408=DIRECTION ( 'NONE',  ( -0.7071067811865487940, 0.7071067811865463515, 0.000000000000000000 ) ) ;
#25409=VERTEX_POINT ( 'NONE', #83017 ) ;
#25410=VECTOR ( 'NONE', #127700, 1000.000000000000227 ) ;
#25411=VECTOR ( 'NONE', #34164, 1000.000000000000000 ) ;
#25412=( BOUNDED_CURVE ( )  B_SPLINE_CURVE ( 3, ( #22485, #66749, #86369, #65349 ),
 .UNSPECIFIED., .F., .F. ) 
 B_SPLINE_CURVE_WITH_KNOTS ( ( 4, 4 ),
 ( 5.106027341939277875, 6.645403452391244414 ),
 .UNSPECIFIED. ) 
 CURVE ( )  GEOMETRIC_REPRESENTATION_ITEM ( )  RATIONAL_B_SPLINE_CURVE ( ( 1.000000000000000000, 0.8120851936182275077, 0.8120851936182275077, 1.000000000000000000 ) ) 
 REPRESENTATION_ITEM ( '' )  );
#25414=VECTOR ( 'NONE', #39657, 1000.000000000000000 ) ;
#25415=PLANE ( 'NONE',  #78346 ) ;
#25416=CARTESIAN_POINT ( 'NONE',  ( 10.17183060077640100, -17.24070752338410628, 4.000000000000000000 ) ) ;
#25417=EDGE_CURVE ( 'NONE', #37944, #24646, #92429, .T. ) ;
#25418=DIRECTION ( 'NONE',  ( -0.7071067811865487940, 0.7071067811865463515, -0.000000000000000000 ) ) ;
#25419=PLANE ( 'NONE',  #26229 ) ;
#25420=ORIENTED_EDGE ( 'NONE', *, *, #106308, .T. ) ;
#25421=ORIENTED_EDGE ( 'NONE', *, *, #18574, .F. ) ;
#25422=VERTEX_POINT ( 'NONE', #49700 ) ;
#25423=ORIENTED_EDGE ( 'NONE', *, *, #18574, .T. ) ;
#25425=DIRECTION ( 'NONE',  ( -0.000000000000000000, 0.000000000000000000, 1.000000000000000000 ) ) ;
#25427=AXIS2_PLACEMENT_3D ( 'NONE', #121083, #85591, #54442 ) ;
#25429=PLANE ( 'NONE',  #88373 ) ;
#25430=EDGE_CURVE ( 'NONE', #49419, #7434, #115584, .T. ) ;
#25431=VECTOR ( 'NONE', #57861, 1000.000000000000000 ) ;
#25432=EDGE_CURVE ( 'NONE', #118358, #133102, #126494, .T. ) ;
#25434=ORIENTED_EDGE ( 'NONE', *, *, #90990, .F. ) ;
#25435=VECTOR ( 'NONE', #38034, 999.9999999999998863 ) ;
#25436=PLANE ( 'NONE',  #16336 ) ;
#25437=ORIENTED_EDGE ( 'NONE', *, *, #27628, .T. ) ;
#25443=DIRECTION ( 'NONE',  ( -0.000000000000000000, 0.3543493200069153248, 0.9351131265310292928 ) ) ;
#25444=FACE_OUTER_BOUND ( 'NONE', #77376, .T. ) ;
#25445=DIRECTION ( 'NONE',  ( 0.3543493200069162685, -0.000000000000000000, -0.9351131265310288487 ) ) ;
#25446=VERTEX_POINT ( 'NONE', #5419 ) ;
#25447=DIRECTION ( 'NONE',  ( 0.000000000000000000, -1.000000000000000000, 0.000000000000000000 ) ) ;
#25448=AXIS2_PLACEMENT_3D ( 'NONE', #70507, #16028, #104497 ) ;
#25449=ORIENTED_EDGE ( 'NONE', *, *, #627, .T. ) ;
#25450=CARTESIAN_POINT ( 'NONE',  ( 33.48921356237309510, -27.52281430457078670, 5.000000000000000000 ) ) ;
#25451=CARTESIAN_POINT ( 'NONE',  ( -15.18398860626900237, 28.73617430169797871, 5.000000000000000000 ) ) ;
#25452=CARTESIAN_POINT ( 'NONE',  ( -12.32816939922344623, -21.74070752338406365, 4.000000000000000000 ) ) ;
#25455=EDGE_CURVE ( 'NONE', #18761, #47327, #27187, .T. ) ;
#25456=ORIENTED_EDGE ( 'NONE', *, *, #120829, .F. ) ;
#25457=CARTESIAN_POINT ( 'NONE',  ( -24.48921356237309510, -27.52281430457072631, 5.000000000000000000 ) ) ;
#25458=CARTESIAN_POINT ( 'NONE',  ( 1.499999999999990896, 3.431123077392149501, 4.000000000000000000 ) ) ;
#25460=EDGE_LOOP ( 'NONE', ( #118039, #101596, #31587, #91255 ) ) ;
#25461=CARTESIAN_POINT ( 'NONE',  ( 16.49999999999988276, -19.91253812416055169, 4.000000000000000000 ) ) ;
#25462=VECTOR ( 'NONE', #7417, 999.9999999999998863 ) ;
#25463=DIRECTION ( 'NONE',  ( -0.6830127018922181881, 0.6830127018922202975, -0.2588190451025214056 ) ) ;
#25464=ORIENTED_EDGE ( 'NONE', *, *, #69492, .F. ) ;
#25465=DIRECTION ( 'NONE',  ( 0.7071067811865487940, 0.7071067811865463515, 0.000000000000000000 ) ) ;
#25466=ORIENTED_EDGE ( 'NONE', *, *, #53013, .F. ) ;
#25467=ORIENTED_EDGE ( 'NONE', *, *, #89622, .T. ) ;
#25471=ORIENTED_EDGE ( 'NONE', *, *, #142481, .F. ) ;
#25472=VECTOR ( 'NONE', #13849, 1000.000000000000000 ) ;
#25474=ADVANCED_FACE ( 'NONE', ( #6114 ), #28649, .T. ) ;
#25475=CARTESIAN_POINT ( 'NONE',  ( 23.99999999999983302, -3.485240976185050243, -4.108735105802342247 ) ) ;
#25476=ORIENTED_EDGE ( 'NONE', *, *, #82342, .F. ) ;
#25477=LINE ( 'NONE', #1042, #117922 ) ;
#25478=EDGE_CURVE ( 'NONE', #35412, #29685, #52514, .T. ) ;
#25479=LINE ( 'NONE', #100214, #35102 ) ;
#25480=CARTESIAN_POINT ( 'NONE',  ( 0.000000000000000000, 0.000000000000000000, 5.000000000000000000 ) ) ;
#25482=DIRECTION ( 'NONE',  ( -0.000000000000000000, -0.3543493200069152693, 0.9351131265310292928 ) ) ;
#25484=CARTESIAN_POINT ( 'NONE',  ( 3.489213562373097322, -27.52281430457057709, 5.000000000000000000 ) ) ;
#25485=DIRECTION ( 'NONE',  ( 0.7071067811865487940, -0.7071067811865463515, 0.000000000000000000 ) ) ;
#25487=ORIENTED_EDGE ( 'NONE', *, *, #99421, .F. ) ;
#25488=ADVANCED_FACE ( 'NONE', ( #42387 ), #106151, .F. ) ;
#25490=ORIENTED_EDGE ( 'NONE', *, *, #54303, .T. ) ;
#25492=VECTOR ( 'NONE', #41877, 1000.000000000000000 ) ;
#25495=VERTEX_POINT ( 'NONE', #53981 ) ;
#25496=PLANE ( 'NONE',  #80362 ) ;
#25497=DIRECTION ( 'NONE',  ( 0.7071067811865487940, -0.7071067811865463515, 0.000000000000000000 ) ) ;
#25499=AXIS2_PLACEMENT_3D ( 'NONE', #44419, #111789, #134259 ) ;
#25500=VECTOR ( 'NONE', #84845, 1000.000000000000000 ) ;
#25501=ORIENTED_EDGE ( 'NONE', *, *, #97510, .T. ) ;
#25502=LINE ( 'NONE', #23360, #18374 ) ;
#25503=DIRECTION ( 'NONE',  ( -0.000000000000000000, 0.000000000000000000, 1.000000000000000000 ) ) ;
#25504=EDGE_CURVE ( 'NONE', #101224, #26788, #19180, .T. ) ;
#25505=DIRECTION ( 'NONE',  ( 1.000000000000000000, 0.000000000000000000, 0.000000000000000000 ) ) ;
#25507=ORIENTED_EDGE ( 'NONE', *, *, #38003, .F. ) ;
#25508=EDGE_CURVE ( 'NONE', #102312, #64028, #20589, .T. ) ;
#25509=DIRECTION ( 'NONE',  ( 0.7071067811865487940, 0.7071067811865463515, 0.000000000000000000 ) ) ;
#25510=LINE ( 'NONE', #135722, #141951 ) ;
#25511=LINE ( 'NONE', #16034, #31219 ) ;
#25512=AXIS2_PLACEMENT_3D ( 'NONE', #123623, #90237, #43901 ) ;
#25514=DIRECTION ( 'NONE',  ( -0.6830127018922180770, -0.6830127018922204085, -0.2588190451025213501 ) ) ;
#25515=CARTESIAN_POINT ( 'NONE',  ( -57.29974487139158157, -27.71228299555246011, 4.000000000000000000 ) ) ;
#25516=CARTESIAN_POINT ( 'NONE',  ( 26.99999999999981171, -21.03360074219752462, 5.000000000000000000 ) ) ;
#25518=DIRECTION ( 'NONE',  ( 0.7071067811865486830, -0.7071067811865464625, -0.000000000000000000 ) ) ;
#25519=LINE ( 'NONE', #82788, #48409 ) ;
#25521=VERTEX_POINT ( 'NONE', #84464 ) ;
#25523=ADVANCED_FACE ( 'NONE', ( #64121 ), #140254, .F. ) ;
#25524=VERTEX_POINT ( 'NONE', #74289 ) ;
#25527=AXIS2_PLACEMENT_3D ( 'NONE', #74577, #86158, #9250 ) ;
#25528=LINE ( 'NONE', #69803, #31602 ) ;
#25531=CARTESIAN_POINT ( 'NONE',  ( -30.79289321881324071, 6.759292476615654799, 5.000000000000000000 ) ) ;
#25535=AXIS2_PLACEMENT_3D ( 'NONE', #95847, #117569, #16112 ) ;
#25537=ORIENTED_EDGE ( 'NONE', *, *, #108444, .F. ) ;
#25538=VECTOR ( 'NONE', #51747, 1000.000000000000227 ) ;
#25539=PLANE ( 'NONE',  #71105 ) ;
#25540=ORIENTED_EDGE ( 'NONE', *, *, #112468, .T. ) ;
#25541=EDGE_CURVE ( 'NONE', #39115, #60184, #142408, .T. ) ;
#25542=CARTESIAN_POINT ( 'NONE',  ( 34.92499999999998295, 3.701285051063797571, 12.01932804697900004 ) ) ;
#25543=AXIS2_PLACEMENT_3D ( 'NONE', #115492, #72082, #124987 ) ;
#25544=CARTESIAN_POINT ( 'NONE',  ( -68.99451991528748351, 28.92564299267986172, 4.000000000000000000 ) ) ;
#25545=PLANE ( 'NONE',  #97293 ) ;
#25546=LINE ( 'NONE', #69083, #106647 ) ;
#25547=VERTEX_POINT ( 'NONE', #86599 ) ;
#25548=ORIENTED_EDGE ( 'NONE', *, *, #35789, .F. ) ;
#25550=DIRECTION ( 'NONE',  ( -0.000000000000000000, -0.3543493200069152693, 0.9351131265310292928 ) ) ;
#25551=CARTESIAN_POINT ( 'NONE',  ( -8.994519915287490619, 28.92564299267944250, 4.000000000000000000 ) ) ;
#25552=LINE ( 'NONE', #61110, #68613 ) ;
#25553=EDGE_CURVE ( 'NONE', #118674, #38224, #118481, .T. ) ;
#25554=EDGE_CURVE ( 'NONE', #108223, #42984, #117741, .T. ) ;
#25555=PLANE ( 'NONE',  #34733 ) ;
#25556=DIRECTION ( 'NONE',  ( 0.7071067811865486830, -0.7071067811865464625, -0.000000000000000000 ) ) ;
#25558=VECTOR ( 'NONE', #136656, 1000.000000000000000 ) ;
#25561=PLANE ( 'NONE',  #89487 ) ;
#25562=ORIENTED_EDGE ( 'NONE', *, *, #127489, .F. ) ;
#25563=ORIENTED_EDGE ( 'NONE', *, *, #70203, .F. ) ;
#25564=AXIS2_PLACEMENT_3D ( 'NONE', #43536, #42133, #89191 ) ;
#25565=CARTESIAN_POINT ( 'NONE',  ( 32.99999999999977263, -13.97847968911257510, -0.1324546996126028109 ) ) ;
#25567=PLANE ( 'NONE',  #137099 ) ;
#25570=CARTESIAN_POINT ( 'NONE',  ( 72.18398860626899705, 28.73617430169837661, 5.000000000000000000 ) ) ;
#25571=AXIS2_PLACEMENT_3D ( 'NONE', #34746, #68129, #22394 ) ;
#25572=FACE_BOUND ( 'NONE', #42557, .T. ) ;
#25573=CARTESIAN_POINT ( 'NONE',  ( 26.99999999999980105, -10.44781430457071458, 5.000000000000000000 ) ) ;
#25574=PLANE ( 'NONE',  #113868 ) ;
#25575=FACE_OUTER_BOUND ( 'NONE', #56046, .T. ) ;
#25576=DIRECTION ( 'NONE',  ( -0.000000000000000000, 0.3543493200069153248, 0.9351131265310292928 ) ) ;
#25578=EDGE_LOOP ( 'NONE', ( #78475, #136860, #39283, #80575 ) ) ;
#25579=AXIS2_PLACEMENT_3D ( 'NONE', #50142, #49455, #48014 ) ;
#25580=CARTESIAN_POINT ( 'NONE',  ( 1.226741607178325033, -11.24070752338417556, 18.24660765846982713 ) ) ;
#25582=ORIENTED_EDGE ( 'NONE', *, *, #1729, .T. ) ;
#25584=ORIENTED_EDGE ( 'NONE', *, *, #97169, .T. ) ;
#25585=( BOUNDED_CURVE ( )  B_SPLINE_CURVE ( 3, ( #13275, #102478, #66275, #976 ),
 .UNSPECIFIED., .F., .T. ) 
 B_SPLINE_CURVE_WITH_KNOTS ( ( 4, 4 ),
 ( 1.864375635226918515, 1.933014472006551188 ),
 .UNSPECIFIED. ) 
 CURVE ( )  GEOMETRIC_REPRESENTATION_ITEM ( )  RATIONAL_B_SPLINE_CURVE ( ( 1.000000000000000000, 0.9996074310407762065, 0.9996074310407762065, 1.000000000000000000 ) ) 
 REPRESENTATION_ITEM ( '' )  );
#25586=LINE ( 'NONE', #101733, #69862 ) ;
#25587=ORIENTED_EDGE ( 'NONE', *, *, #127769, .T. ) ;
#25588=PLANE ( 'NONE',  #93026 ) ;
#25589=VECTOR ( 'NONE', #31571, 1000.000000000000227 ) ;
#25590=CARTESIAN_POINT ( 'NONE',  ( 26.20710678118636494, -20.24070752338407075, 5.000000000000000000 ) ) ;
#25592=LINE ( 'NONE', #24190, #91828 ) ;
#25593=LINE ( 'NONE', #3129, #25064 ) ;
#25594=CARTESIAN_POINT ( 'NONE',  ( -25.01899999999999835, 3.174999999999998046, 4.000000000000000000 ) ) ;
#25595=DIRECTION ( 'NONE',  ( 0.7071067811865487940, 0.7071067811865463515, 0.000000000000000000 ) ) ;
#25596=DIRECTION ( 'NONE',  ( -0.7071067811865486830, -0.7071067811865464625, 0.000000000000000000 ) ) ;
#25597=DIRECTION ( 'NONE',  ( -0.7071067811865486830, -0.7071067811865464625, -0.000000000000000000 ) ) ;
#25598=ORIENTED_EDGE ( 'NONE', *, *, #93574, .T. ) ;
#25599=VECTOR ( 'NONE', #14602, 1000.000000000000000 ) ;
#25600=VECTOR ( 'NONE', #101270, 1000.000000000000000 ) ;
#25602=VERTEX_POINT ( 'NONE', #75020 ) ;
#25604=LINE ( 'NONE', #94427, #72860 ) ;
#25606=ORIENTED_EDGE ( 'NONE', *, *, #90156, .F. ) ;
#25607=VECTOR ( 'NONE', #128687, 999.9999999999998863 ) ;
#25608=ORIENTED_EDGE ( 'NONE', *, *, #67381, .F. ) ;
#25609=VERTEX_POINT ( 'NONE', #96699 ) ;
#25610=EDGE_CURVE ( 'NONE', #57920, #35696, #61999, .T. ) ;
#25612=CARTESIAN_POINT ( 'NONE',  ( 0.7928932188134563130, -5.240707523384228850, 5.000000000000000000 ) ) ;
#25613=ORIENTED_EDGE ( 'NONE', *, *, #122211, .T. ) ;
#25615=DIRECTION ( 'NONE',  ( -0.3543493200069162685, -0.000000000000000000, -0.9351131265310288487 ) ) ;
#25616=CARTESIAN_POINT ( 'NONE',  ( 35.99451991528749772, 28.92564299267963079, 4.000000000000000000 ) ) ;
#25618=PLANE ( 'NONE',  #84297 ) ;
#25619=ORIENTED_EDGE ( 'NONE', *, *, #36841, .T. ) ;
#25620=EDGE_CURVE ( 'NONE', #93569, #10232, #119195, .T. ) ;
#25621=DIRECTION ( 'NONE',  ( -0.000000000000000000, 0.000000000000000000, 1.000000000000000000 ) ) ;
#25622=LINE ( 'NONE', #68465, #28100 ) ;
#25624=DIRECTION ( 'NONE',  ( 1.000000000000000000, 0.000000000000000000, 0.000000000000000000 ) ) ;
#25625=PLANE ( 'NONE',  #21696 ) ;
#25626=EDGE_LOOP ( 'NONE', ( #143073, #90581, #141062, #127998 ) ) ;
#25627=ORIENTED_EDGE ( 'NONE', *, *, #112981, .T. ) ;
#25629=CARTESIAN_POINT ( 'NONE',  ( -34.92500000000001137, 12.75929247661558996, 4.255531930566247567 ) ) ;
#25630=CARTESIAN_POINT ( 'NONE',  ( -34.92500000000001137, -22.22500000000000142, 4.000000000000000000 ) ) ;
#25631=ADVANCED_FACE ( 'NONE', ( #106889 ), #8958, .F. ) ;
#25632=ORIENTED_EDGE ( 'NONE', *, *, #14998, .F. ) ;
#25633=AXIS2_PLACEMENT_3D ( 'NONE', #120954, #110069, #31817 ) ;
#25634=DIRECTION ( 'NONE',  ( 1.000000000000000000, 0.000000000000000000, 0.000000000000000000 ) ) ;
#25636=VECTOR ( 'NONE', #57673, 1000.000000000000227 ) ;
#25639=CARTESIAN_POINT ( 'NONE',  ( 5.510786437626906675, -27.52281430457051314, 5.000000000000000000 ) ) ;
#25640=DIRECTION ( 'NONE',  ( -0.000000000000000000, 0.000000000000000000, 1.000000000000000000 ) ) ;
#25641=ORIENTED_EDGE ( 'NONE', *, *, #65820, .T. ) ;
#25642=EDGE_CURVE ( 'NONE', #106829, #27961, #131519, .T. ) ;
#25643=CARTESIAN_POINT ( 'NONE',  ( -34.45011844616454511, 0.002304141593953373465, 5.000000000000000888 ) ) ;
#25644=VECTOR ( 'NONE', #69946, 1000.000000000000227 ) ;
#25645=DIRECTION ( 'NONE',  ( -0.7071067811865486830, 0.7071067811865464625, 0.000000000000000000 ) ) ;
#25647=CARTESIAN_POINT ( 'NONE',  ( 42.48921356237308800, -27.52281430457085065, 5.000000000000000000 ) ) ;
#25648=DIRECTION ( 'NONE',  ( 0.7071067811865486830, -0.7071067811865464625, -0.000000000000000000 ) ) ;
#25651=VERTEX_POINT ( 'NONE', #134382 ) ;
#25652=EDGE_CURVE ( 'NONE', #94488, #41471, #65585, .T. ) ;
#25653=PLANE ( 'NONE',  #54887 ) ;
#25654=CARTESIAN_POINT ( 'NONE',  ( 54.18398860626899705, 28.73617430169825226, 5.000000000000000000 ) ) ;
#25656=CARTESIAN_POINT ( 'NONE',  ( 29.99999999999979750, 5.587461875839193404, 4.000000000000000000 ) ) ;
#25657=VECTOR ( 'NONE', #7646, 1000.000000000000000 ) ;
#25658=LINE ( 'NONE', #79387, #104023 ) ;
#25659=LINE ( 'NONE', #78630, #89981 ) ;
#25660=LINE ( 'NONE', #80780, #39810 ) ;
#25661=ORIENTED_EDGE ( 'NONE', *, *, #101279, .T. ) ;
#25662=EDGE_CURVE ( 'NONE', #100222, #117346, #132259, .T. ) ;
#25664=CARTESIAN_POINT ( 'NONE',  ( -40.26506670282026334, 12.75929247661558996, 18.34774599283965557 ) ) ;
#25667=DIRECTION ( 'NONE',  ( -0.7071067811865486830, -0.7071067811865464625, 0.000000000000000000 ) ) ;
#25668=EDGE_CURVE ( 'NONE', #38684, #114903, #143100, .T. ) ;
#25669=ADVANCED_FACE ( 'NONE', ( #13273 ), #77851, .F. ) ;
#25670=CARTESIAN_POINT ( 'NONE',  ( 10.17183060077640455, -8.240707523384196875, 4.000000000000000000 ) ) ;
#25672=CARTESIAN_POINT ( 'NONE',  ( 77.99451991528749772, 28.92564299267992567, 4.000000000000000000 ) ) ;
#25673=ORIENTED_EDGE ( 'NONE', *, *, #97328, .F. ) ;
#25674=VECTOR ( 'NONE', #86812, 1000.000000000000000 ) ;
#25675=LINE ( 'NONE', #124994, #38539 ) ;
#25676=ADVANCED_FACE ( 'NONE', ( #90139 ), #57546, .F. ) ;
#25677=LINE ( 'NONE', #71346, #136377 ) ;
#25678=LINE ( 'NONE', #56227, #134605 ) ;
#25679=FACE_OUTER_BOUND ( 'NONE', #81395, .T. ) ;
#25680=ADVANCED_FACE ( 'NONE', ( #43794 ), #109755, .F. ) ;
#25681=DIRECTION ( 'NONE',  ( -0.6830127018922181881, 0.6830127018922202975, -0.2588190451025214056 ) ) ;
#25683=ORIENTED_EDGE ( 'NONE', *, *, #3135, .T. ) ;
#25684=ADVANCED_FACE ( 'NONE', ( #88008 ), #35083, .F. ) ;
#25685=ORIENTED_EDGE ( 'NONE', *, *, #135187, .F. ) ;
#25689=VECTOR ( 'NONE', #138399, 1000.000000000000000 ) ;
#25690=DIRECTION ( 'NONE',  ( -0.7071067811865486830, 0.7071067811865464625, 0.000000000000000000 ) ) ;
#25691=DIRECTION ( 'NONE',  ( 0.7071067811865486830, -0.7071067811865464625, -0.000000000000000000 ) ) ;
#25693=CARTESIAN_POINT ( 'NONE',  ( -29.18753812416032289, -22.22500000000000142, 4.000000000000000000 ) ) ;
#25694=ORIENTED_EDGE ( 'NONE', *, *, #72112, .T. ) ;
#25696=EDGE_CURVE ( 'NONE', #68874, #44719, #79324, .T. ) ;
#25697=LINE ( 'NONE', #91674, #14594 ) ;
#25698=DIRECTION ( 'NONE',  ( 1.000000000000000000, 0.000000000000000000, 0.000000000000000000 ) ) ;
#25699=PLANE ( 'NONE',  #33546 ) ;
#25701=VECTOR ( 'NONE', #96395, 1000.000000000000227 ) ;
#25702=EDGE_CURVE ( 'NONE', #56955, #63125, #22023, .T. ) ;
#25703=PLANE ( 'NONE',  #46784 ) ;
#25704=AXIS2_PLACEMENT_3D ( 'NONE', #77358, #121517, #34528 ) ;
#25705=VECTOR ( 'NONE', #76779, 1000.000000000000000 ) ;
#25709=ORIENTED_EDGE ( 'NONE', *, *, #72740, .T. ) ;
#25710=VECTOR ( 'NONE', #70292, 1000.000000000000000 ) ;
#25711=EDGE_LOOP ( 'NONE', ( #18441, #79046, #11225, #117144 ) ) ;
#25712=AXIS2_PLACEMENT_3D ( 'NONE', #108368, #133056, #130187 ) ;
#25713=AXIS2_PLACEMENT_3D ( 'NONE', #29755, #53691, #118177 ) ;
#25714=VECTOR ( 'NONE', #65166, 1000.000000000000227 ) ;
#25716=LINE ( 'NONE', #67847, #70791 ) ;
#25717=CARTESIAN_POINT ( 'NONE',  ( -20.99451991528748707, 28.92564299267952777, 4.000000000000000000 ) ) ;
#25720=LINE ( 'NONE', #69993, #135531 ) ;
#25721=ORIENTED_EDGE ( 'NONE', *, *, #42137, .T. ) ;
#25722=FACE_OUTER_BOUND ( 'NONE', #14171, .T. ) ;
#25723=CARTESIAN_POINT ( 'NONE',  ( 0.000000000000000000, 0.000000000000000000, 5.000000000000000000 ) ) ;
#25724=LINE ( 'NONE', #69997, #12330 ) ;
#25725=AXIS2_PLACEMENT_3D ( 'NONE', #136077, #110724, #81007 ) ;
#25726=ADVANCED_FACE ( 'NONE', ( #122039 ), #66272, .F. ) ;
#25727=ORIENTED_EDGE ( 'NONE', *, *, #5153, .F. ) ;
#25728=EDGE_CURVE ( 'NONE', #52039, #90340, #135118, .T. ) ;
#25730=AXIS2_PLACEMENT_3D ( 'NONE', #6824, #140253, #94577 ) ;
#25731=DIRECTION ( 'NONE',  ( -0.000000000000000000, 0.000000000000000000, 1.000000000000000000 ) ) ;
#25732=EDGE_CURVE ( 'NONE', #40790, #81729, #22707, .T. ) ;
#25733=CARTESIAN_POINT ( 'NONE',  ( 1.499999999999987566, -2.568876922607790103, 4.000000000000000000 ) ) ;
#25735=CARTESIAN_POINT ( 'NONE',  ( -25.17183060077629264, 0.7592924766157173044, 4.000000000000000000 ) ) ;
#25736=DIRECTION ( 'NONE',  ( 0.7071067811865487940, 0.7071067811865463515, 0.000000000000000000 ) ) ;
#25737=EDGE_LOOP ( 'NONE', ( #118478, #139867, #120670, #82514 ) ) ;
#25738=EDGE_LOOP ( 'NONE', ( #120267, #92285, #10055, #109661 ) ) ;
#25739=DIRECTION ( 'NONE',  ( -0.7071067811865487940, 0.7071067811865463515, 0.000000000000000000 ) ) ;
#25740=EDGE_CURVE ( 'NONE', #26466, #45983, #111156, .T. ) ;
#25745=VERTEX_POINT ( 'NONE', #99569 ) ;
#25746=VECTOR ( 'NONE', #80380, 1000.000000000000227 ) ;
#25747=FACE_OUTER_BOUND ( 'NONE', #120181, .T. ) ;
#25748=DIRECTION ( 'NONE',  ( -0.7071067811865486830, -0.7071067811865464625, -0.000000000000000000 ) ) ;
#25750=ORIENTED_EDGE ( 'NONE', *, *, #142025, .T. ) ;
#25751=FACE_BOUND ( 'NONE', #135601, .T. ) ;
#25752=VECTOR ( 'NONE', #50118, 1000.000000000000000 ) ;
#25756=DIRECTION ( 'NONE',  ( 0.7071067811865486830, -0.7071067811865464625, -0.000000000000000000 ) ) ;
#25758=VERTEX_POINT ( 'NONE', #44546 ) ;
#25759=VECTOR ( 'NONE', #128121, 999.9999999999998863 ) ;
#25760=EDGE_LOOP ( 'NONE', ( #110190, #3416, #89841, #77109 ) ) ;
#25762=ORIENTED_EDGE ( 'NONE', *, *, #6635, .T. ) ;
#25764=VECTOR ( 'NONE', #2151, 1000.000000000000227 ) ;
#25765=DIRECTION ( 'NONE',  ( 0.7071067811865487940, 0.7071067811865463515, -0.000000000000000000 ) ) ;
#25766=VECTOR ( 'NONE', #42637, 1000.000000000000000 ) ;
#25768=DIRECTION ( 'NONE',  ( 0.000000000000000000, 1.000000000000000000, 0.000000000000000000 ) ) ;
#25769=ORIENTED_EDGE ( 'NONE', *, *, #73282, .T. ) ;
#25772=DIRECTION ( 'NONE',  ( -0.000000000000000000, 0.3543493200069153248, 0.9351131265310292928 ) ) ;
#25775=DIRECTION ( 'NONE',  ( 0.7071067811865486830, -0.7071067811865464625, -0.000000000000000000 ) ) ;
#25777=CARTESIAN_POINT ( 'NONE',  ( 12.18398860626900060, 28.73617430169795739, 5.000000000000000000 ) ) ;
#25780=ORIENTED_EDGE ( 'NONE', *, *, #138182, .T. ) ;
#25781=ORIENTED_EDGE ( 'NONE', *, *, #92911, .T. ) ;
#25782=EDGE_CURVE ( 'NONE', #50596, #22720, #56135, .T. ) ;
#25783=ADVANCED_FACE ( 'NONE', ( #89429 ), #34342, .T. ) ;
#25784=VERTEX_POINT ( 'NONE', #16877 ) ;
#25786=VECTOR ( 'NONE', #40674, 1000.000000000000227 ) ;
#25787=VERTEX_POINT ( 'NONE', #115422 ) ;
#25788=EDGE_CURVE ( 'NONE', #50127, #1245, #116182, .T. ) ;
#25789=EDGE_CURVE ( 'NONE', #61139, #106547, #102475, .T. ) ;
#25791=DIRECTION ( 'NONE',  ( 0.7071067811865487940, 0.7071067811865463515, 0.000000000000000000 ) ) ;
#25792=ORIENTED_EDGE ( 'NONE', *, *, #119689, .T. ) ;
#25793=ADVANCED_FACE ( 'NONE', ( #27025 ), #25588, .F. ) ;
#25794=FACE_OUTER_BOUND ( 'NONE', #11194, .T. ) ;
#25795=ORIENTED_EDGE ( 'NONE', *, *, #35700, .F. ) ;
#25796=FACE_OUTER_BOUND ( 'NONE', #143286, .T. ) ;
#25797=VECTOR ( 'NONE', #12086, 1000.000000000000227 ) ;
#25798=DIRECTION ( 'NONE',  ( -0.000000000000000000, 0.3543493200069153248, 0.9351131265310292928 ) ) ;
#25800=VERTEX_POINT ( 'NONE', #113309 ) ;
#25802=CARTESIAN_POINT ( 'NONE',  ( -42.18398860626899705, 28.73617430169816700, 5.000000000000000000 ) ) ;
#25803=AXIS2_PLACEMENT_3D ( 'NONE', #118318, #28492, #86440 ) ;
#25804=LINE ( 'NONE', #62559, #79924 ) ;
#25805=EDGE_CURVE ( 'NONE', #92363, #27557, #58291, .T. ) ;
#25806=VECTOR ( 'NONE', #43955, 999.9999999999998863 ) ;
#25807=VERTEX_POINT ( 'NONE', #71271 ) ;
#25808=CARTESIAN_POINT ( 'NONE',  ( -51.18398860626899705, 28.73617430169823095, 5.000000000000000000 ) ) ;
#25810=ORIENTED_EDGE ( 'NONE', *, *, #58757, .T. ) ;
#25811=VERTEX_POINT ( 'NONE', #92267 ) ;
#25812=VECTOR ( 'NONE', #36037, 999.9999999999998863 ) ;
#25813=VECTOR ( 'NONE', #91842, 1000.000000000000000 ) ;
#25814=AXIS2_PLACEMENT_3D ( 'NONE', #11374, #100583, #79590 ) ;
#25817=AXIS2_PLACEMENT_3D ( 'NONE', #10126, #86284, #107983 ) ;
#25819=DIRECTION ( 'NONE',  ( -0.7071067811865486830, 0.7071067811865464625, 0.000000000000000000 ) ) ;
#25820=PLANE ( 'NONE',  #122772 ) ;
#25821=CARTESIAN_POINT ( 'NONE',  ( 2.356812572482602786, -20.24070752338407786, 21.22881796311213520 ) ) ;
#25822=VERTEX_POINT ( 'NONE', #81447 ) ;
#25824=PLANE ( 'NONE',  #65652 ) ;
#25827=CARTESIAN_POINT ( 'NONE',  ( 68.99451991528748351, 28.92564299267986172, 4.000000000000000000 ) ) ;
#25830=ORIENTED_EDGE ( 'NONE', *, *, #105147, .T. ) ;
#25831=ORIENTED_EDGE ( 'NONE', *, *, #26247, .T. ) ;
#25832=EDGE_CURVE ( 'NONE', #33166, #42524, #103160, .T. ) ;
#25833=ORIENTED_EDGE ( 'NONE', *, *, #89071, .F. ) ;
#25836=DIRECTION ( 'NONE',  ( 0.7071067811865487940, -0.7071067811865463515, 0.000000000000000000 ) ) ;
#25838=FACE_OUTER_BOUND ( 'NONE', #106280, .T. ) ;
#25839=CARTESIAN_POINT ( 'NONE',  ( 9.489213562373095101, -27.52281430457062328, 5.000000000000000000 ) ) ;
#25842=EDGE_CURVE ( 'NONE', #28959, #11288, #127042, .T. ) ;
#25844=CARTESIAN_POINT ( 'NONE',  ( -3.475126127850438618, 14.25929247661557397, 9.797011795316629801 ) ) ;
#25845=CARTESIAN_POINT ( 'NONE',  ( 7.828169399223476432, 21.75929247661548871, 4.000000000000000000 ) ) ;
#25846=DIRECTION ( 'NONE',  ( 0.7071067811865487940, -0.7071067811865463515, 0.000000000000000000 ) ) ;
#25847=ADVANCED_FACE ( 'NONE', ( #5254 ), #69130, .F. ) ;
#25848=AXIS2_PLACEMENT_3D ( 'NONE', #69700, #136344, #113883 ) ;
#25849=PLANE ( 'NONE',  #51110 ) ;
#25850=ORIENTED_EDGE ( 'NONE', *, *, #25136, .F. ) ;
#25851=AXIS2_PLACEMENT_3D ( 'NONE', #22272, #65862, #110017 ) ;
#25852=VERTEX_POINT ( 'NONE', #15401 ) ;
#25853=ADVANCED_FACE ( 'NONE', ( #4494 ), #48799, .F. ) ;
#25854=DIRECTION ( 'NONE',  ( 0.7071067811865487940, 0.7071067811865463515, -0.000000000000000000 ) ) ;
#25855=CARTESIAN_POINT ( 'NONE',  ( -36.29974487139159578, -27.71228299555231445, 4.000000000000000000 ) ) ;
#25857=FACE_OUTER_BOUND ( 'NONE', #90155, .T. ) ;
#25858=DIRECTION ( 'NONE',  ( 0.7071067811865487940, -0.7071067811865463515, 0.000000000000000000 ) ) ;
#25859=ORIENTED_EDGE ( 'NONE', *, *, #103131, .T. ) ;
#25860=CARTESIAN_POINT ( 'NONE',  ( 31.49999999999977973, 11.52377502935406106, -1.522421517564156890 ) ) ;
#25861=VERTEX_POINT ( 'NONE', #84980 ) ;
#25862=LINE ( 'NONE', #125907, #134723 ) ;
#25864=ORIENTED_EDGE ( 'NONE', *, *, #8711, .T. ) ;
#25866=DIRECTION ( 'NONE',  ( 0.6830127018922180770, -0.6830127018922204085, -0.2588190451025213501 ) ) ;
#25868=CARTESIAN_POINT ( 'NONE',  ( 14.99999999999990941, 4.384688058510586295, -7.090945410444652985 ) ) ;
#25869=DIRECTION ( 'NONE',  ( 0.7071067811865487940, 0.7071067811865463515, -0.000000000000000000 ) ) ;
#25871=EDGE_CURVE ( 'NONE', #41224, #118405, #64659, .T. ) ;
#25872=CARTESIAN_POINT ( 'NONE',  ( 2.816011393730999401, 28.73617430169785436, 5.000000000000000000 ) ) ;
#25873=LINE ( 'NONE', #48343, #84326 ) ;
#25876=AXIS2_PLACEMENT_3D ( 'NONE', #55890, #109528, #77640 ) ;
#25878=FACE_OUTER_BOUND ( 'NONE', #129067, .T. ) ;
#25879=VECTOR ( 'NONE', #1566, 1000.000000000000000 ) ;
#25880=CARTESIAN_POINT ( 'NONE',  ( 40.22674160717809855, -11.24070752338416490, 18.24660765846991950 ) ) ;
#25881=ORIENTED_EDGE ( 'NONE', *, *, #132212, .F. ) ;
#25882=CARTESIAN_POINT ( 'NONE',  ( -33.18398860626899705, 28.73617430169810305, 5.000000000000000000 ) ) ;
#25884=ADVANCED_FACE ( 'NONE', ( #8103 ), #140768, .F. ) ;
#25886=AXIS2_PLACEMENT_3D ( 'NONE', #17911, #137607, #50585 ) ;
#25887=CARTESIAN_POINT ( 'NONE',  ( 2.999999999999975131, -0.2811185226894337141, -5.995736974527521745 ) ) ;
#25888=LINE ( 'NONE', #70159, #127044 ) ;
#25889=LINE ( 'NONE', #126605, #12244 ) ;
#25890=AXIS2_PLACEMENT_3D ( 'NONE', #84347, #25640, #4536 ) ;
#25894=( BOUNDED_CURVE ( )  B_SPLINE_CURVE ( 3, ( #124123, #45176, #36406, #69050 ),
 .UNSPECIFIED., .F., .T. ) 
 B_SPLINE_CURVE_WITH_KNOTS ( ( 4, 4 ),
 ( 4.628641526727098388, 4.642507259593578794 ),
 .UNSPECIFIED. ) 
 CURVE ( )  GEOMETRIC_REPRESENTATION_ITEM ( )  RATIONAL_B_SPLINE_CURVE ( ( 1.000000000000000000, 0.9999839785185119512, 0.9999839785185119512, 1.000000000000000000 ) ) 
 REPRESENTATION_ITEM ( '' )  );
#25895=FACE_OUTER_BOUND ( 'NONE', #1912, .T. ) ;
#25896=EDGE_CURVE ( 'NONE', #83399, #22749, #116891, .T. ) ;
#25897=ORIENTED_EDGE ( 'NONE', *, *, #132761, .T. ) ;
#25898=DIRECTION ( 'NONE',  ( -0.7071067811865486830, -0.7071067811865464625, 0.000000000000000000 ) ) ;
#25900=DIRECTION ( 'NONE',  ( -0.7071067811865486830, -0.7071067811865464625, 0.000000000000000000 ) ) ;
#25901=ORIENTED_EDGE ( 'NONE', *, *, #14145, .F. ) ;
#25902=DIRECTION ( 'NONE',  ( -0.6830127018922181881, 0.6830127018922202975, -0.2588190451025214056 ) ) ;
#25903=CARTESIAN_POINT ( 'NONE',  ( -34.49999999999976552, 13.46425560840034841, 4.994342998332165884 ) ) ;
#25904=VECTOR ( 'NONE', #97139, 999.9999999999998863 ) ;
#25906=FACE_OUTER_BOUND ( 'NONE', #77892, .T. ) ;
#25907=ORIENTED_EDGE ( 'NONE', *, *, #44575, .T. ) ;
#25908=EDGE_CURVE ( 'NONE', #82619, #17176, #53803, .T. ) ;
#25910=ORIENTED_EDGE ( 'NONE', *, *, #86404, .T. ) ;
#25912=ORIENTED_EDGE ( 'NONE', *, *, #8372, .T. ) ;
#25913=ADVANCED_FACE ( 'NONE', ( #29170 ), #95127, .F. ) ;
#25914=CARTESIAN_POINT ( 'NONE',  ( -20.29289321881331887, -9.740707523384186217, 5.000000000000000000 ) ) ;
#25915=CARTESIAN_POINT ( 'NONE',  ( -7.499999999999945821, 21.05218569542895324, 5.000000000000000000 ) ) ;
#25916=CARTESIAN_POINT ( 'NONE',  ( 3.469446951953614189E-15, -6.033600742197680056, 5.000000000000000000 ) ) ;
#25917=VERTEX_POINT ( 'NONE', #20412 ) ;
#25918=VECTOR ( 'NONE', #124267, 1000.000000000000000 ) ;
#25921=LINE ( 'NONE', #34665, #69737 ) ;
#25922=ADVANCED_FACE ( 'NONE', ( #119715 ), #17564, .F. ) ;
#25923=AXIS2_PLACEMENT_3D ( 'NONE', #46913, #122986, #99792 ) ;
#25924=VECTOR ( 'NONE', #45076, 1000.000000000000227 ) ;
#25926=EDGE_CURVE ( 'NONE', #60486, #103852, #141507, .T. ) ;
#25927=EDGE_LOOP ( 'NONE', ( #126639, #84838, #50952, #12614 ) ) ;
#25928=LINE ( 'NONE', #24490, #65196 ) ;
#25929=VECTOR ( 'NONE', #27132, 1000.000000000000000 ) ;
#25930=LINE ( 'NONE', #131299, #124259 ) ;
#25931=LINE ( 'NONE', #15030, #612 ) ;
#25932=VECTOR ( 'NONE', #129453, 1000.000000000000000 ) ;
#25934=VECTOR ( 'NONE', #46444, 1000.000000000000000 ) ;
#25935=ORIENTED_EDGE ( 'NONE', *, *, #128341, .F. ) ;
#25936=ORIENTED_EDGE ( 'NONE', *, *, #81730, .F. ) ;
#25938=EDGE_CURVE ( 'NONE', #121113, #42588, #72739, .T. ) ;
#25940=CARTESIAN_POINT ( 'NONE',  ( -0.3281693992235254487, -18.74070752338409562, 4.000000000000000000 ) ) ;
#25943=DIRECTION ( 'NONE',  ( 0.6830127018922180770, -0.6830127018922204085, -0.2588190451025213501 ) ) ;
#25944=CARTESIAN_POINT ( 'NONE',  ( 4.499999999999970690, 0.4311230773921797543, 4.000000000000000000 ) ) ;
#25945=ORIENTED_EDGE ( 'NONE', *, *, #20117, .F. ) ;
#25946=VERTEX_POINT ( 'NONE', #108840 ) ;
#25948=ORIENTED_EDGE ( 'NONE', *, *, #15510, .T. ) ;
#25949=AXIS2_PLACEMENT_3D ( 'NONE', #33826, #65030, #86775 ) ;
#25950=AXIS2_PLACEMENT_3D ( 'NONE', #31640, #109185, #99010 ) ;
#25951=CARTESIAN_POINT ( 'NONE',  ( 4.499999999999972466, 19.39370406404967540, 1.459788787078191374 ) ) ;
#25953=DIRECTION ( 'NONE',  ( 0.6830127018922181881, 0.6830127018922202975, -0.2588190451025214056 ) ) ;
#25954=DIRECTION ( 'NONE',  ( -0.7071067811865486830, 0.7071067811865464625, 0.000000000000000000 ) ) ;
#25956=LINE ( 'NONE', #47060, #29952 ) ;
#25957=VECTOR ( 'NONE', #135731, 999.9999999999998863 ) ;
#25958=DIRECTION ( 'NONE',  ( 0.7071067811865487940, 0.7071067811865463515, 0.000000000000000000 ) ) ;
#25959=ORIENTED_EDGE ( 'NONE', *, *, #22211, .T. ) ;
#25960=ADVANCED_FACE ( 'NONE', ( #7394 ), #40778, .F. ) ;
#25961=DIRECTION ( 'NONE',  ( 0.7071067811865487940, 0.7071067811865463515, 0.000000000000000000 ) ) ;
#25962=FACE_OUTER_BOUND ( 'NONE', #73195, .T. ) ;
#25963=VERTEX_POINT ( 'NONE', #74852 ) ;
#25965=EDGE_LOOP ( 'NONE', ( #121718, #42606, #67254, #95329 ) ) ;
#25966=EDGE_CURVE ( 'NONE', #49695, #49753, #9526, .T. ) ;
#25967=ORIENTED_EDGE ( 'NONE', *, *, #39935, .T. ) ;
#25968=CARTESIAN_POINT ( 'NONE',  ( -3.707106781186514599, 11.25929247661560240, 5.000000000000000000 ) ) ;
#25969=VERTEX_POINT ( 'NONE', #119027 ) ;
#25970=ORIENTED_EDGE ( 'NONE', *, *, #76244, .F. ) ;
#25971=LINE ( 'NONE', #121861, #7028 ) ;
#25973=ORIENTED_EDGE ( 'NONE', *, *, #1558, .F. ) ;
#25974=EDGE_CURVE ( 'NONE', #108223, #36313, #84303, .T. ) ;
#25976=CARTESIAN_POINT ( 'NONE',  ( 27.29974487139158512, -27.71228299555225405, 4.000000000000000000 ) ) ;
#25977=LINE ( 'NONE', #36838, #37991 ) ;
#25978=EDGE_CURVE ( 'NONE', #101519, #86499, #142928, .T. ) ;
#25980=FACE_OUTER_BOUND ( 'NONE', #33499, .T. ) ;
#25981=EDGE_CURVE ( 'NONE', #18783, #129767, #45092, .T. ) ;
#25982=PLANE ( 'NONE',  #20480 ) ;
#25984=AXIS2_PLACEMENT_3D ( 'NONE', #34793, #121062, #46415 ) ;
#25985=EDGE_CURVE ( 'NONE', #17335, #96047, #43610, .T. ) ;
#25986=DIRECTION ( 'NONE',  ( -0.7071067811865486830, -0.7071067811865464625, 0.000000000000000000 ) ) ;
#25987=DIRECTION ( 'NONE',  ( -0.6830127018922181881, 0.6830127018922202975, -0.2588190451025214056 ) ) ;
#25988=DIRECTION ( 'NONE',  ( -0.7071067811865486830, -0.7071067811865464625, 0.000000000000000000 ) ) ;
#25989=EDGE_CURVE ( 'NONE', #29835, #135832, #132321, .T. ) ;
#25990=EDGE_LOOP ( 'NONE', ( #17409, #52601, #114989, #63644 ) ) ;
#25991=CARTESIAN_POINT ( 'NONE',  ( 8.999999999999941380, 10.55218569542906160, 5.000000000000000000 ) ) ;
#25992=CARTESIAN_POINT ( 'NONE',  ( -36.18398860626899705, 28.73617430169812437, 5.000000000000000000 ) ) ;
#25993=VERTEX_POINT ( 'NONE', #98005 ) ;
#25994=VERTEX_POINT ( 'NONE', #33488 ) ;
#25996=LINE ( 'NONE', #126031, #100488 ) ;
#25997=ORIENTED_EDGE ( 'NONE', *, *, #55411, .T. ) ;
#25998=DIRECTION ( 'NONE',  ( -0.7071067811865486830, -0.7071067811865464625, 0.000000000000000000 ) ) ;
#25999=LINE ( 'NONE', #138326, #98721 ) ;
#26000=DIRECTION ( 'NONE',  ( 0.7071067811865487940, 0.7071067811865463515, 0.000000000000000000 ) ) ;
#26002=CARTESIAN_POINT ( 'NONE',  ( 8.999999999999948486, 14.58746187583909837, 4.000000000000000000 ) ) ;
#26003=DIRECTION ( 'NONE',  ( -0.7071067811865487940, 0.7071067811865463515, 0.000000000000000000 ) ) ;
#26006=VECTOR ( 'NONE', #44999, 1000.000000000000000 ) ;
#26007=EDGE_LOOP ( 'NONE', ( #42356, #80521, #47230, #93347 ) ) ;
#26009=FACE_OUTER_BOUND ( 'NONE', #21733, .T. ) ;
#26012=DIRECTION ( 'NONE',  ( -0.7071067811865486830, 0.7071067811865464625, 0.000000000000000000 ) ) ;
#26013=ORIENTED_EDGE ( 'NONE', *, *, #142999, .F. ) ;
#26014=ORIENTED_EDGE ( 'NONE', *, *, #138417, .F. ) ;
#26015=ORIENTED_EDGE ( 'NONE', *, *, #75777, .T. ) ;
#26016=DIRECTION ( 'NONE',  ( -0.6830127018922181881, 0.6830127018922202975, -0.2588190451025214056 ) ) ;
#26017=LINE ( 'NONE', #6342, #55746 ) ;
#26018=AXIS2_PLACEMENT_3D ( 'NONE', #21921, #68333, #112504 ) ;
#26020=DIRECTION ( 'NONE',  ( 0.7071067811865486830, -0.7071067811865464625, -0.000000000000000000 ) ) ;
#26021=DIRECTION ( 'NONE',  ( -0.7071067811865486830, -0.7071067811865464625, -0.000000000000000000 ) ) ;
#26022=ORIENTED_EDGE ( 'NONE', *, *, #125315, .F. ) ;
#26023=CARTESIAN_POINT ( 'NONE',  ( 22.17665910159958997, 5.259292476615662792, 15.86257073897092518 ) ) ;
#26024=AXIS2_PLACEMENT_3D ( 'NONE', #103347, #5454, #59193 ) ;
#26025=CARTESIAN_POINT ( 'NONE',  ( 29.29387692260784704, 22.22500000000000497, 4.000000000000000000 ) ) ;
#26026=VECTOR ( 'NONE', #85484, 1000.000000000000000 ) ;
#26027=CARTESIAN_POINT ( 'NONE',  ( 8.207106781186489286, -5.240707523384232402, 5.000000000000000000 ) ) ;
#26028=CARTESIAN_POINT ( 'NONE',  ( 34.92499999999998295, -9.281509562795639212, 4.759050581649326261 ) ) ;
#26029=EDGE_CURVE ( 'NONE', #75514, #15522, #122588, .T. ) ;
#26030=ORIENTED_EDGE ( 'NONE', *, *, #85244, .F. ) ;
#26035=VERTEX_POINT ( 'NONE', #100849 ) ;
#26036=EDGE_CURVE ( 'NONE', #75052, #74837, #23263, .T. ) ;
#26037=CARTESIAN_POINT ( 'NONE',  ( -60.18398860626900415, 28.73617430169829490, 5.000000000000000000 ) ) ;
#26039=ORIENTED_EDGE ( 'NONE', *, *, #20414, .F. ) ;
#26040=DIRECTION ( 'NONE',  ( -0.000000000000000000, -0.000000000000000000, 1.000000000000000000 ) ) ;
#26041=DIRECTION ( 'NONE',  ( 0.6830127018922181881, 0.6830127018922202975, -0.2588190451025214056 ) ) ;
#26042=ORIENTED_EDGE ( 'NONE', *, *, #125743, .T. ) ;
#26043=CARTESIAN_POINT ( 'NONE',  ( 15.18398860626900237, 28.73617430169797871, 5.000000000000000000 ) ) ;
#26045=ADVANCED_FACE ( 'NONE', ( #32026 ), #34903, .F. ) ;
#26046=DIRECTION ( 'NONE',  ( -0.6830127018922180770, -0.6830127018922204085, -0.2588190451025213501 ) ) ;
#26047=CARTESIAN_POINT ( 'NONE',  ( 0.000000000000000000, 0.000000000000000000, 5.000000000000000000 ) ) ;
#26049=FACE_OUTER_BOUND ( 'NONE', #12058, .T. ) ;
#26051=EDGE_CURVE ( 'NONE', #90068, #26803, #32762, .T. ) ;
#26053=CARTESIAN_POINT ( 'NONE',  ( -2.816011393730999401, 28.73617430169785436, 5.000000000000000000 ) ) ;
#26054=CARTESIAN_POINT ( 'NONE',  ( 23.22995720542188991, 21.73644205237998506, 5.000000000000000888 ) ) ;
#26056=CARTESIAN_POINT ( 'NONE',  ( -1.499999999999984013, -14.94781430457067728, 5.000000000000000000 ) ) ;
#26057=CARTESIAN_POINT ( 'NONE',  ( 45.48921356237309510, -27.52281430457087197, 5.000000000000000000 ) ) ;
#26059=CARTESIAN_POINT ( 'NONE',  ( 59.99451991528749772, 28.92564299267980132, 4.000000000000000000 ) ) ;
#26060=VERTEX_POINT ( 'NONE', #10950 ) ;
#26061=VECTOR ( 'NONE', #40264, 1000.000000000000000 ) ;
#26062=ORIENTED_EDGE ( 'NONE', *, *, #78689, .T. ) ;
#26065=VERTEX_POINT ( 'NONE', #121163 ) ;
#26067=VECTOR ( 'NONE', #94786, 1000.000000000000000 ) ;
#26068=DIRECTION ( 'NONE',  ( 0.7071067811865487940, 0.7071067811865463515, -0.000000000000000000 ) ) ;
#26069=CARTESIAN_POINT ( 'NONE',  ( 1.998069433179001653, -22.22500000000000142, 4.500000000000000888 ) ) ;
#26071=VECTOR ( 'NONE', #134876, 1000.000000000000000 ) ;
#26073=ORIENTED_EDGE ( 'NONE', *, *, #3588, .T. ) ;
#26074=CARTESIAN_POINT ( 'NONE',  ( 28.49999999999980105, -10.04351517176476172, -1.623559851933757958 ) ) ;
#26075=FACE_OUTER_BOUND ( 'NONE', #88484, .T. ) ;
#26076=CARTESIAN_POINT ( 'NONE',  ( 11.81601139373100651, 28.73617430169779041, 5.000000000000000000 ) ) ;
#26078=EDGE_CURVE ( 'NONE', #80179, #112545, #79429, .T. ) ;
#26080=CARTESIAN_POINT ( 'NONE',  ( -48.48921356237309510, -27.52281430457089328, 5.000000000000000000 ) ) ;
#26081=ADVANCED_FACE ( 'NONE', ( #10258 ), #110981, .F. ) ;
#26082=DIRECTION ( 'NONE',  ( 0.7071067811865486830, -0.7071067811865464625, -0.000000000000000000 ) ) ;
#26083=DIRECTION ( 'NONE',  ( -0.000000000000000000, 0.3543493200069153248, 0.9351131265310292928 ) ) ;
#26084=PLANE ( 'NONE',  #45246 ) ;
#26085=DIRECTION ( 'NONE',  ( -0.7071067811865486830, -0.7071067811865464625, -0.000000000000000000 ) ) ;
#26086=CARTESIAN_POINT ( 'NONE',  ( 12.18398860626900060, 28.73617430169795739, 5.000000000000000000 ) ) ;
#26087=PLANE ( 'NONE',  #15178 ) ;
#26089=EDGE_CURVE ( 'NONE', #4447, #55801, #114567, .T. ) ;
#26090=ORIENTED_EDGE ( 'NONE', *, *, #10838, .F. ) ;
#26091=VERTEX_POINT ( 'NONE', #81996 ) ;
#26093=ORIENTED_EDGE ( 'NONE', *, *, #80863, .T. ) ;
#26094=VECTOR ( 'NONE', #132413, 1000.000000000000000 ) ;
#26095=CARTESIAN_POINT ( 'NONE',  ( -19.49999999999986500, 12.43112307739205669, 4.000000000000000000 ) ) ;
#26096=DIRECTION ( 'NONE',  ( -0.7071067811865486830, -0.7071067811865464625, 0.000000000000000000 ) ) ;
#26097=VERTEX_POINT ( 'NONE', #113863 ) ;
#26098=PLANE ( 'NONE',  #67612 ) ;
#26099=FACE_OUTER_BOUND ( 'NONE', #5474, .T. ) ;
#26100=EDGE_CURVE ( 'NONE', #31004, #60184, #15236, .T. ) ;
#26103=ORIENTED_EDGE ( 'NONE', *, *, #86740, .T. ) ;
#26104=EDGE_LOOP ( 'NONE', ( #115477, #91178, #36005, #51860 ) ) ;
#26106=VECTOR ( 'NONE', #47029, 1000.000000000000000 ) ;
#26108=CARTESIAN_POINT ( 'NONE',  ( 39.18398860626899705, 28.73617430169814568, 5.000000000000000000 ) ) ;
#26109=ORIENTED_EDGE ( 'NONE', *, *, #126522, .T. ) ;
#26110=ORIENTED_EDGE ( 'NONE', *, *, #23606, .F. ) ;
#26111=ORIENTED_EDGE ( 'NONE', *, *, #87183, .F. ) ;
#26112=CARTESIAN_POINT ( 'NONE',  ( 9.781626882924877364, 21.74787736706807095, 4.999607392498048419 ) ) ;
#26113=EDGE_CURVE ( 'NONE', #19552, #141993, #115982, .T. ) ;
#26114=VECTOR ( 'NONE', #82780, 999.9999999999998863 ) ;
#26116=ORIENTED_EDGE ( 'NONE', *, *, #99351, .F. ) ;
#26118=ORIENTED_EDGE ( 'NONE', *, *, #19109, .F. ) ;
#26120=VECTOR ( 'NONE', #103045, 1000.000000000000000 ) ;
#26121=VECTOR ( 'NONE', #137986, 1000.000000000000000 ) ;
#26122=DIRECTION ( 'NONE',  ( -0.7071067811865486830, 0.7071067811865464625, 0.000000000000000000 ) ) ;
#26123=VECTOR ( 'NONE', #50234, 999.9999999999998863 ) ;
#26125=ORIENTED_EDGE ( 'NONE', *, *, #126518, .F. ) ;
#26126=DIRECTION ( 'NONE',  ( -0.000000000000000000, 0.000000000000000000, 1.000000000000000000 ) ) ;
#26127=EDGE_CURVE ( 'NONE', #54291, #29863, #136325, .T. ) ;
#26129=VECTOR ( 'NONE', #18542, 1000.000000000000000 ) ;
#26131=FACE_OUTER_BOUND ( 'NONE', #18069, .T. ) ;
#26132=LINE ( 'NONE', #34883, #102243 ) ;
#26133=LINE ( 'NONE', #114549, #92757 ) ;
#26134=FACE_BOUND ( 'NONE', #53422, .T. ) ;
#26135=EDGE_LOOP ( 'NONE', ( #135552, #18643, #37335, #5293 ) ) ;
#26136=FACE_OUTER_BOUND ( 'NONE', #96626, .T. ) ;
#26137=CARTESIAN_POINT ( 'NONE',  ( 3.489213562373097322, -27.52281430457057709, 5.000000000000000000 ) ) ;
#26138=DIRECTION ( 'NONE',  ( -0.7071067811865486830, -0.7071067811865464625, 0.000000000000000000 ) ) ;
#26139=VERTEX_POINT ( 'NONE', #92098 ) ;
#26140=CARTESIAN_POINT ( 'NONE',  ( 2.816011393730999401, 28.73617430169785436, 5.000000000000000000 ) ) ;
#26141=ORIENTED_EDGE ( 'NONE', *, *, #90866, .F. ) ;
#26142=ORIENTED_EDGE ( 'NONE', *, *, #25620, .F. ) ;
#26143=ORIENTED_EDGE ( 'NONE', *, *, #142163, .T. ) ;
#26144=EDGE_CURVE ( 'NONE', #51152, #8757, #124039, .T. ) ;
#26146=ORIENTED_EDGE ( 'NONE', *, *, #79394, .T. ) ;
#26147=VECTOR ( 'NONE', #47481, 999.9999999999998863 ) ;
#26148=PLANE ( 'NONE',  #76186 ) ;
#26152=CARTESIAN_POINT ( 'NONE',  ( 2.994519915287485734, 28.92564299267940342, 4.000000000000000000 ) ) ;
#26153=VERTEX_POINT ( 'NONE', #14557 ) ;
#26154=EDGE_CURVE ( 'NONE', #106936, #29169, #93548, .T. ) ;
#26155=DIRECTION ( 'NONE',  ( 0.7071067811865487940, -0.7071067811865463515, 0.000000000000000000 ) ) ;
#26157=AXIS2_PLACEMENT_3D ( 'NONE', #33162, #32415, #120083 ) ;
#26160=CARTESIAN_POINT ( 'NONE',  ( -10.49999999999992539, 6.431123077392117082, 4.000000000000000000 ) ) ;
#26161=AXIS2_PLACEMENT_3D ( 'NONE', #106763, #6704, #50986 ) ;
#26162=DIRECTION ( 'NONE',  ( 0.6830127018922180770, -0.6830127018922204085, -0.2588190451025213501 ) ) ;
#26163=EDGE_CURVE ( 'NONE', #73090, #3334, #46526, .T. ) ;
#26164=ORIENTED_EDGE ( 'NONE', *, *, #71165, .F. ) ;
#26165=ORIENTED_EDGE ( 'NONE', *, *, #68898, .T. ) ;
#26166=EDGE_LOOP ( 'NONE', ( #94228, #33451, #39347, #94884 ) ) ;
#26168=PLANE ( 'NONE',  #58830 ) ;
#26169=ORIENTED_EDGE ( 'NONE', *, *, #16404, .T. ) ;
#26170=EDGE_LOOP ( 'NONE', ( #121047, #93144, #126093, #34921 ) ) ;
#26171=PLANE ( 'NONE',  #132377 ) ;
#26172=FACE_OUTER_BOUND ( 'NONE', #100355, .T. ) ;
#26173=ADVANCED_FACE ( 'NONE', ( #71103 ), #15932, .F. ) ;
#26174=ADVANCED_FACE ( 'NONE', ( #52173 ), #62363, .F. ) ;
#26175=LINE ( 'NONE', #38474, #64851 ) ;
#26176=ORIENTED_EDGE ( 'NONE', *, *, #83036, .T. ) ;
#26178=VERTEX_POINT ( 'NONE', #29692 ) ;
#26179=EDGE_CURVE ( 'NONE', #43903, #52144, #60969, .T. ) ;
#26180=CARTESIAN_POINT ( 'NONE',  ( -3.328169399223503966, 8.259292476615637923, 4.000000000000000000 ) ) ;
#26181=VECTOR ( 'NONE', #84188, 1000.000000000000000 ) ;
#26182=LINE ( 'NONE', #70444, #77430 ) ;
#26186=CARTESIAN_POINT ( 'NONE',  ( 0.000000000000000000, 0.000000000000000000, 5.000000000000000000 ) ) ;
#26189=EDGE_LOOP ( 'NONE', ( #120899, #79337, #135358 ) ) ;
#26191=EDGE_LOOP ( 'NONE', ( #9931, #143466, #26763, #142696 ) ) ;
#26192=ORIENTED_EDGE ( 'NONE', *, *, #104244, .F. ) ;
#26193=CARTESIAN_POINT ( 'NONE',  ( -7.499999999999944045, -17.94781430457063820, 5.000000000000000000 ) ) ;
#26194=VECTOR ( 'NONE', #128591, 1000.000000000000227 ) ;
#26195=CARTESIAN_POINT ( 'NONE',  ( 18.32816939922340893, 17.25929247661554200, 4.000000000000000000 ) ) ;
#26196=DIRECTION ( 'NONE',  ( 0.7071067811865486830, -0.7071067811865464625, -0.000000000000000000 ) ) ;
#26199=LINE ( 'NONE', #39958, #62162 ) ;
#26200=DIRECTION ( 'NONE',  ( -0.000000000000000000, 0.3543493200069153248, 0.9351131265310292928 ) ) ;
#26201=FACE_OUTER_BOUND ( 'NONE', #40766, .T. ) ;
#26202=EDGE_CURVE ( 'NONE', #100179, #127004, #105129, .T. ) ;
#26203=ORIENTED_EDGE ( 'NONE', *, *, #70832, .F. ) ;
#26204=DIRECTION ( 'NONE',  ( 0.6830127018922180770, -0.6830127018922204085, -0.2588190451025213501 ) ) ;
#26206=LINE ( 'NONE', #90765, #93274 ) ;
#26207=VERTEX_POINT ( 'NONE', #118857 ) ;
#26208=DIRECTION ( 'NONE',  ( 0.7071067811865486830, -0.7071067811865464625, -0.000000000000000000 ) ) ;
#26209=ORIENTED_EDGE ( 'NONE', *, *, #31623, .T. ) ;
#26210=ORIENTED_EDGE ( 'NONE', *, *, #44231, .F. ) ;
#26211=EDGE_CURVE ( 'NONE', #71184, #43157, #84129, .T. ) ;
#26212=VECTOR ( 'NONE', #140527, 999.9999999999998863 ) ;
#26213=PLANE ( 'NONE',  #2976 ) ;
#26214=DIRECTION ( 'NONE',  ( -4.681814790819591790E-17, -0.3543493200069152693, 0.9351131265310292928 ) ) ;
#26215=ORIENTED_EDGE ( 'NONE', *, *, #60740, .T. ) ;
#26216=CARTESIAN_POINT ( 'NONE',  ( 33.18398860626899705, 28.73617430169810305, 5.000000000000000000 ) ) ;
#26217=EDGE_CURVE ( 'NONE', #129157, #41854, #129728, .T. ) ;
#26218=PLANE ( 'NONE',  #109959 ) ;
#26219=ORIENTED_EDGE ( 'NONE', *, *, #53473, .F. ) ;
#26220=DIRECTION ( 'NONE',  ( -0.7071067811865486830, -0.7071067811865464625, 0.000000000000000000 ) ) ;
#26222=ADVANCED_FACE ( 'NONE', ( #6476 ), #40605, .F. ) ;
#26224=VECTOR ( 'NONE', #5669, 1000.000000000000000 ) ;
#26225=DIRECTION ( 'NONE',  ( 0.7071067811865487940, 0.7071067811865463515, 0.000000000000000000 ) ) ;
#26227=CARTESIAN_POINT ( 'NONE',  ( 10.49999999999992717, -13.91253812416061209, 4.000000000000000000 ) ) ;
#26228=EDGE_LOOP ( 'NONE', ( #45202, #101419, #42025, #66753, #17994, #139240 ) ) ;
#26229=AXIS2_PLACEMENT_3D ( 'NONE', #2216, #79149, #55221 ) ;
#26230=ORIENTED_EDGE ( 'NONE', *, *, #137422, .F. ) ;
#26231=ORIENTED_EDGE ( 'NONE', *, *, #7341, .F. ) ;
#26233=ORIENTED_EDGE ( 'NONE', *, *, #137442, .T. ) ;
#26235=EDGE_CURVE ( 'NONE', #75711, #39393, #50055, .T. ) ;
#26236=EDGE_LOOP ( 'NONE', ( #99124, #60311, #83034, #37414 ) ) ;
#26237=VECTOR ( 'NONE', #95808, 1000.000000000000000 ) ;
#26240=LINE ( 'NONE', #105212, #41677 ) ;
#26241=VERTEX_POINT ( 'NONE', #74669 ) ;
#26244=CARTESIAN_POINT ( 'NONE',  ( -3.489213562373097322, -27.52281430457057709, 5.000000000000000000 ) ) ;
#26245=FACE_OUTER_BOUND ( 'NONE', #117675, .T. ) ;
#26247=EDGE_CURVE ( 'NONE', #75231, #13355, #39169, .T. ) ;
#26249=CARTESIAN_POINT ( 'NONE',  ( 3.489213562373097322, -27.52281430457057709, 5.000000000000000000 ) ) ;
#26250=DIRECTION ( 'NONE',  ( 0.6830127018922180770, -0.6830127018922204085, -0.2588190451025213501 ) ) ;
#26251=CARTESIAN_POINT ( 'NONE',  ( -28.49999999999980460, -16.53360074219757081, 5.000000000000000000 ) ) ;
#26253=LINE ( 'NONE', #59613, #54420 ) ;
#26254=CARTESIAN_POINT ( 'NONE',  ( 32.99999999999977263, -7.068876922607732816, 4.000000000000000000 ) ) ;
#26255=CARTESIAN_POINT ( 'NONE',  ( -54.48921356237310221, -27.52281430457093236, 5.000000000000000000 ) ) ;
#26258=VECTOR ( 'NONE', #137853, 1000.000000000000000 ) ;
#26260=EDGE_LOOP ( 'NONE', ( #27462, #140780, #85406, #29643 ) ) ;
#26261=ORIENTED_EDGE ( 'NONE', *, *, #49349, .F. ) ;
#26263=ORIENTED_EDGE ( 'NONE', *, *, #114155, .F. ) ;
#26264=ORIENTED_EDGE ( 'NONE', *, *, #81670, .T. ) ;
#26265=DIRECTION ( 'NONE',  ( 0.7071067811865486830, -0.7071067811865464625, -0.000000000000000000 ) ) ;
#26266=LINE ( 'NONE', #43916, #8367 ) ;
#26267=ORIENTED_EDGE ( 'NONE', *, *, #29839, .F. ) ;
#26268=CARTESIAN_POINT ( 'NONE',  ( 69.18398860626899705, 28.73617430169835529, 5.000000000000000000 ) ) ;
#26271=DIRECTION ( 'NONE',  ( 1.000000000000000000, 0.000000000000000000, 0.000000000000000000 ) ) ;
#26273=EDGE_CURVE ( 'NONE', #91335, #44987, #42037, .T. ) ;
#26274=AXIS2_PLACEMENT_3D ( 'NONE', #119229, #41683, #130864 ) ;
#26276=FACE_OUTER_BOUND ( 'NONE', #135873, .T. ) ;
#26278=LINE ( 'NONE', #15354, #31136 ) ;
#26279=DIRECTION ( 'NONE',  ( -4.681814790819591790E-17, -0.3543493200069152693, 0.9351131265310292928 ) ) ;
#26281=AXIS2_PLACEMENT_3D ( 'NONE', #29376, #49025, #139620 ) ;
#26283=ORIENTED_EDGE ( 'NONE', *, *, #56019, .T. ) ;
#26284=EDGE_CURVE ( 'NONE', #56703, #138242, #41289, .T. ) ;
#26286=PLANE ( 'NONE',  #116468 ) ;
#26287=ADVANCED_FACE ( 'NONE', ( #61658 ), #75372, .F. ) ;
#26288=DIRECTION ( 'NONE',  ( -0.7071067811865486830, -0.7071067811865464625, 0.000000000000000000 ) ) ;
#26289=DIRECTION ( 'NONE',  ( -0.000000000000000000, -0.3543493200069152693, 0.9351131265310292928 ) ) ;
#26290=VECTOR ( 'NONE', #66447, 1000.000000000000000 ) ;
#26291=AXIS2_PLACEMENT_3D ( 'NONE', #27973, #128709, #61363 ) ;
#26292=VECTOR ( 'NONE', #85165, 1000.000000000000227 ) ;
#26296=ORIENTED_EDGE ( 'NONE', *, *, #39237, .F. ) ;
#26297=ORIENTED_EDGE ( 'NONE', *, *, #107346, .F. ) ;
#26299=LINE ( 'NONE', #71970, #118687 ) ;
#26300=VERTEX_POINT ( 'NONE', #29005 ) ;
#26301=EDGE_CURVE ( 'NONE', #116545, #40105, #8619, .T. ) ;
#26302=( BOUNDED_CURVE ( )  B_SPLINE_CURVE ( 3, ( #94795, #82530, #73791, #106372 ),
 .UNSPECIFIED., .F., .F. ) 
 B_SPLINE_CURVE_WITH_KNOTS ( ( 4, 4 ),
 ( 5.920967161967926273, 7.341195215986580536 ),
 .UNSPECIFIED. ) 
 CURVE ( )  GEOMETRIC_REPRESENTATION_ITEM ( )  RATIONAL_B_SPLINE_CURVE ( ( 1.000000000000000000, 0.8388583629366737071, 0.8388583629366737071, 1.000000000000000000 ) ) 
 REPRESENTATION_ITEM ( '' )  );
#26304=ORIENTED_EDGE ( 'NONE', *, *, #11695, .T. ) ;
#26305=FACE_OUTER_BOUND ( 'NONE', #139190, .T. ) ;
#26306=CARTESIAN_POINT ( 'NONE',  ( 18.18398860626898994, 28.73617430169800002, 5.000000000000000000 ) ) ;
#26308=CARTESIAN_POINT ( 'NONE',  ( -33.15612307739218778, -22.22500000000000142, 4.000000000000000000 ) ) ;
#26309=FACE_BOUND ( 'NONE', #87626, .T. ) ;
#26310=CARTESIAN_POINT ( 'NONE',  ( -34.92500000000001137, 22.22500000000000142, 4.000000000000000000 ) ) ;
#26311=CARTESIAN_POINT ( 'NONE',  ( -21.79289321881330110, -8.240707523384198652, 5.000000000000000000 ) ) ;
#26312=CARTESIAN_POINT ( 'NONE',  ( 2.999999999999984457, 19.55218569542897100, 5.000000000000000000 ) ) ;
#26313=VECTOR ( 'NONE', #59121, 1000.000000000000000 ) ;
#26314=DIRECTION ( 'NONE',  ( -0.000000000000000000, 0.000000000000000000, 1.000000000000000000 ) ) ;
#26315=LINE ( 'NONE', #4481, #124558 ) ;
#26316=VERTEX_POINT ( 'NONE', #18821 ) ;
#26317=DIRECTION ( 'NONE',  ( -0.000000000000000000, -0.3543493200069152693, 0.9351131265310292928 ) ) ;
#26318=VERTEX_POINT ( 'NONE', #51479 ) ;
#26319=ADVANCED_FACE ( 'NONE', ( #95674 ), #105815, .F. ) ;
#26320=ADVANCED_FACE ( 'NONE', ( #94946 ), #73237, .T. ) ;
#26323=ORIENTED_EDGE ( 'NONE', *, *, #25250, .F. ) ;
#26324=LINE ( 'NONE', #69863, #7282 ) ;
#26325=ADVANCED_FACE ( 'NONE', ( #5785 ), #84808, .F. ) ;
#26326=CARTESIAN_POINT ( 'NONE',  ( -19.05000000000000071, 3.174999999999997158, 5.000000000000000000 ) ) ;
#26327=ORIENTED_EDGE ( 'NONE', *, *, #90415, .T. ) ;
#26328=DIRECTION ( 'NONE',  ( -0.7071067811865486830, -0.7071067811865464625, 0.000000000000000000 ) ) ;
#26329=ADVANCED_FACE ( 'NONE', ( #64483 ), #10093, .T. ) ;
#26330=EDGE_CURVE ( 'NONE', #56258, #95511, #33330, .T. ) ;
#26331=VECTOR ( 'NONE', #65958, 999.9999999999998863 ) ;
#26332=CARTESIAN_POINT ( 'NONE',  ( 23.67183060077630685, -6.740707523384209310, 4.000000000000000000 ) ) ;
#26333=LINE ( 'NONE', #138671, #4115 ) ;
#26334=DIRECTION ( 'NONE',  ( 0.7071067811865487940, 0.7071067811865463515, 0.000000000000000000 ) ) ;
#26336=LINE ( 'NONE', #90149, #97195 ) ;
#26337=EDGE_LOOP ( 'NONE', ( #33210, #70369, #127038, #34689 ) ) ;
#26338=ORIENTED_EDGE ( 'NONE', *, *, #78247, .F. ) ;
#26339=ORIENTED_EDGE ( 'NONE', *, *, #134738, .T. ) ;
#26340=LINE ( 'NONE', #91590, #26543 ) ;
#26341=ORIENTED_EDGE ( 'NONE', *, *, #1747, .T. ) ;
#26342=ORIENTED_EDGE ( 'NONE', *, *, #12462, .F. ) ;
#26343=ORIENTED_EDGE ( 'NONE', *, *, #9227, .T. ) ;
#26344=ADVANCED_FACE ( 'NONE', ( #99220 ), #23080, .F. ) ;
#26345=EDGE_CURVE ( 'NONE', #44351, #123046, #44176, .T. ) ;
#26346=DIRECTION ( 'NONE',  ( 0.7071067811865487940, 0.7071067811865463515, 0.000000000000000000 ) ) ;
#26347=ORIENTED_EDGE ( 'NONE', *, *, #62331, .T. ) ;
#26348=CARTESIAN_POINT ( 'NONE',  ( -8.287690060339658160, -21.73547319004781642, 4.999917730833664642 ) ) ;
#26349=VECTOR ( 'NONE', #7007, 1000.000000000000227 ) ;
#26350=EDGE_CURVE ( 'NONE', #16457, #398, #142760, .T. ) ;
#26351=DIRECTION ( 'NONE',  ( 0.6830127018922180770, -0.6830127018922204085, -0.2588190451025213501 ) ) ;
#26354=CARTESIAN_POINT ( 'NONE',  ( 34.49999999999976552, 0.05432934483094861711, 4.994342998332161443 ) ) ;
#26355=ORIENTED_EDGE ( 'NONE', *, *, #14967, .F. ) ;
#26356=LINE ( 'NONE', #70614, #78155 ) ;
#26357=CARTESIAN_POINT ( 'NONE',  ( 20.99999999999986144, -13.44781430457069149, 5.000000000000000000 ) ) ;
#26358=LINE ( 'NONE', #59718, #128313 ) ;
#26359=EDGE_CURVE ( 'NONE', #43634, #11154, #98534, .T. ) ;
#26360=DIRECTION ( 'NONE',  ( 0.3543493200069162685, -0.000000000000000000, -0.9351131265310288487 ) ) ;
#26362=DIRECTION ( 'NONE',  ( -0.7071067811865486830, 0.7071067811865464625, 0.000000000000000000 ) ) ;
#26363=ORIENTED_EDGE ( 'NONE', *, *, #26688, .T. ) ;
#26364=LINE ( 'NONE', #72773, #137539 ) ;
#26365=LINE ( 'NONE', #39391, #74792 ) ;
#26366=VECTOR ( 'NONE', #27056, 1000.000000000000000 ) ;
#26367=CARTESIAN_POINT ( 'NONE',  ( -42.48921356237308800, -27.52281430457085065, 5.000000000000000000 ) ) ;
#26368=ORIENTED_EDGE ( 'NONE', *, *, #49153, .F. ) ;
#26370=CARTESIAN_POINT ( 'NONE',  ( -42.18398860626899705, 28.73617430169816700, 5.000000000000000000 ) ) ;
#26371=VECTOR ( 'NONE', #84849, 1000.000000000000000 ) ;
#26372=VECTOR ( 'NONE', #31439, 1000.000000000000000 ) ;
#26373=FACE_OUTER_BOUND ( 'NONE', #15651, .T. ) ;
#26374=LINE ( 'NONE', #61871, #41870 ) ;
#26375=CARTESIAN_POINT ( 'NONE',  ( -29.99999999999979039, 9.631307414974292769, -9.079085613539609412 ) ) ;
#26376=EDGE_CURVE ( 'NONE', #93689, #140843, #45622, .T. ) ;
#26377=EDGE_LOOP ( 'NONE', ( #96649, #61699, #41578, #44743 ) ) ;
#26378=DIRECTION ( 'NONE',  ( -0.3543493200069162685, -0.000000000000000000, -0.9351131265310288487 ) ) ;
#26379=DIRECTION ( 'NONE',  ( 0.6830127018922181881, 0.6830127018922202975, -0.2588190451025214056 ) ) ;
#26380=CARTESIAN_POINT ( 'NONE',  ( -5.999999999999970690, -22.22500000000000142, 4.412002311790005571 ) ) ;
#26381=VECTOR ( 'NONE', #50730, 1000.000000000000000 ) ;
#26382=CARTESIAN_POINT ( 'NONE',  ( -22.41489890804854568, -1.755427004171023819, 4.190031470807584313 ) ) ;
#26383=CARTESIAN_POINT ( 'NONE',  ( -23.99999999999982947, -19.22509904557638549, 1.855685503482122023 ) ) ;
#26384=VECTOR ( 'NONE', #12435, 1000.000000000000227 ) ;
#26385=EDGE_LOOP ( 'NONE', ( #86912, #119066, #20322, #96573 ) ) ;
#26386=EDGE_CURVE ( 'NONE', #129048, #73712, #9339, .T. ) ;
#26387=ORIENTED_EDGE ( 'NONE', *, *, #110151, .T. ) ;
#26388=DIRECTION ( 'NONE',  ( 0.6830127018922181881, 0.6830127018922202975, -0.2588190451025214056 ) ) ;
#26389=CARTESIAN_POINT ( 'NONE',  ( -20.99999999999984723, -21.41253812416053748, 4.000000000000000000 ) ) ;
#26390=AXIS2_PLACEMENT_3D ( 'NONE', #124206, #24885, #100323 ) ;
#26391=ADVANCED_FACE ( 'NONE', ( #97823 ), #32584, .F. ) ;
#26393=PLANE ( 'NONE',  #115336 ) ;
#26394=VECTOR ( 'NONE', #99986, 999.9999999999998863 ) ;
#26395=FACE_OUTER_BOUND ( 'NONE', #10304, .T. ) ;
#26396=DIRECTION ( 'NONE',  ( -1.000000000000000000, 0.000000000000000000, 0.000000000000000000 ) ) ;
#26397=DIRECTION ( 'NONE',  ( 0.7071067811865486830, -0.7071067811865464625, -0.000000000000000000 ) ) ;
#26398=ORIENTED_EDGE ( 'NONE', *, *, #123034, .F. ) ;
#26400=CARTESIAN_POINT ( 'NONE',  ( 24.18398860626899705, 28.73617430169804265, 5.000000000000000000 ) ) ;
#26404=PLANE ( 'NONE',  #134432 ) ;
#26406=ORIENTED_EDGE ( 'NONE', *, *, #33962, .T. ) ;
#26407=ORIENTED_EDGE ( 'NONE', *, *, #49458, .T. ) ;
#26408=DIRECTION ( 'NONE',  ( -0.6830127018922181881, 0.6830127018922202975, -0.2588190451025214056 ) ) ;
#26409=ORIENTED_EDGE ( 'NONE', *, *, #95288, .T. ) ;
#26410=VECTOR ( 'NONE', #63663, 1000.000000000000000 ) ;
#26411=DIRECTION ( 'NONE',  ( 0.7071067811865486830, -0.7071067811865464625, -0.000000000000000000 ) ) ;
#26412=LINE ( 'NONE', #69209, #43773 ) ;
#26413=CARTESIAN_POINT ( 'NONE',  ( 5.816011393731002066, 28.73617430169783304, 5.000000000000000000 ) ) ;
#26414=FACE_OUTER_BOUND ( 'NONE', #40103, .T. ) ;
#26415=CARTESIAN_POINT ( 'NONE',  ( 6.423278458063501617, 11.25929247661559529, 17.85071094206583098 ) ) ;
#26417=ORIENTED_EDGE ( 'NONE', *, *, #73373, .F. ) ;
#26418=PLANE ( 'NONE',  #81136 ) ;
#26419=CARTESIAN_POINT ( 'NONE',  ( 21.48921356237309155, -27.52281430457070499, 5.000000000000000000 ) ) ;
#26420=CARTESIAN_POINT ( 'NONE',  ( -32.99999999999977263, 2.342191155542415970, -5.001666872980010226 ) ) ;
#26421=FACE_OUTER_BOUND ( 'NONE', #72930, .T. ) ;
#26423=VECTOR ( 'NONE', #45636, 1000.000000000000000 ) ;
#26424=PLANE ( 'NONE',  #6763 ) ;
#26425=ORIENTED_EDGE ( 'NONE', *, *, #111968, .T. ) ;
#26426=ORIENTED_EDGE ( 'NONE', *, *, #41238, .T. ) ;
#26428=LINE ( 'NONE', #93107, #70220 ) ;
#26429=DIRECTION ( 'NONE',  ( -0.7071067811865486830, 0.7071067811865464625, 0.000000000000000000 ) ) ;
#26430=CARTESIAN_POINT ( 'NONE',  ( 13.10362284818588741, 2.655808543615126638, 5.000000000000000000 ) ) ;
#26431=ORIENTED_EDGE ( 'NONE', *, *, #107056, .T. ) ;
#26432=VECTOR ( 'NONE', #73406, 999.9999999999998863 ) ;
#26433=CARTESIAN_POINT ( 'NONE',  ( -30.29974487139158867, -27.71228299555227537, 4.000000000000000000 ) ) ;
#26436=PLANE ( 'NONE',  #87622 ) ;
#26437=VERTEX_POINT ( 'NONE', #633 ) ;
#26438=VERTEX_POINT ( 'NONE', #120992 ) ;
#26440=DIRECTION ( 'NONE',  ( 0.7071067811865487940, 0.7071067811865463515, 0.000000000000000000 ) ) ;
#26441=LINE ( 'NONE', #25717, #125396 ) ;
#26444=CARTESIAN_POINT ( 'NONE',  ( -5.671830600776424092, -21.74070752338406010, 4.000000000000000000 ) ) ;
#26446=ORIENTED_EDGE ( 'NONE', *, *, #38896, .T. ) ;
#26447=EDGE_CURVE ( 'NONE', #27246, #126680, #65952, .T. ) ;
#26448=DIRECTION ( 'NONE',  ( 0.7071067811865486830, -0.7071067811865464625, -0.000000000000000000 ) ) ;
#26449=DIRECTION ( 'NONE',  ( 0.7071067811865487940, 0.7071067811865463515, 0.000000000000000000 ) ) ;
#26450=FACE_OUTER_BOUND ( 'NONE', #83181, .T. ) ;
#26451=VECTOR ( 'NONE', #109936, 1000.000000000000227 ) ;
#26453=ORIENTED_EDGE ( 'NONE', *, *, #133030, .T. ) ;
#26454=ORIENTED_EDGE ( 'NONE', *, *, #19393, .F. ) ;
#26455=EDGE_CURVE ( 'NONE', #21745, #6566, #67360, .T. ) ;
#26456=CARTESIAN_POINT ( 'NONE',  ( 7.998069433178966570, -22.22500000000000142, 4.500000000000000888 ) ) ;
#26457=VECTOR ( 'NONE', #19973, 999.9999999999998863 ) ;
#26458=FACE_OUTER_BOUND ( 'NONE', #3102, .T. ) ;
#26460=DIRECTION ( 'NONE',  ( -0.000000000000000000, 0.000000000000000000, 1.000000000000000000 ) ) ;
#26461=ORIENTED_EDGE ( 'NONE', *, *, #83965, .T. ) ;
#26462=ORIENTED_EDGE ( 'NONE', *, *, #26607, .F. ) ;
#26463=CARTESIAN_POINT ( 'NONE',  ( -11.14994871458968539, -8.240707523384186217, 17.25253755692236268 ) ) ;
#26464=LINE ( 'NONE', #70715, #62893 ) ;
#26465=EDGE_CURVE ( 'NONE', #119913, #97364, #111551, .T. ) ;
#26466=VERTEX_POINT ( 'NONE', #120244 ) ;
#26467=AXIS2_PLACEMENT_3D ( 'NONE', #91302, #127459, #70286 ) ;
#26468=CARTESIAN_POINT ( 'NONE',  ( 34.92499999999998295, 11.07784511950550410, 0.7759263132492005832 ) ) ;
#26469=VERTEX_POINT ( 'NONE', #12228 ) ;
#26470=CARTESIAN_POINT ( 'NONE',  ( 15.29177708983037931, -15.74070752338412049, 19.73771281079101314 ) ) ;
#26471=LINE ( 'NONE', #127196, #98015 ) ;
#26472=ADVANCED_FACE ( 'NONE', ( #20962 ), #56517, .F. ) ;
#26474=FACE_BOUND ( 'NONE', #14127, .T. ) ;
#26475=CARTESIAN_POINT ( 'NONE',  ( 48.29974487139158867, -27.71228299555239971, 4.000000000000000000 ) ) ;
#26476=LINE ( 'NONE', #70727, #44365 ) ;
#26477=CARTESIAN_POINT ( 'NONE',  ( -33.18398860626899705, 28.73617430169810305, 5.000000000000000000 ) ) ;
#26478=FACE_OUTER_BOUND ( 'NONE', #101312, .T. ) ;
#26479=( BOUNDED_CURVE ( )  B_SPLINE_CURVE ( 3, ( #28037, #114319, #103425, #136073 ),
 .UNSPECIFIED., .F., .T. ) 
 B_SPLINE_CURVE_WITH_KNOTS ( ( 4, 4 ),
 ( 4.350170835173023498, 4.500739107949268458 ),
 .UNSPECIFIED. ) 
 CURVE ( )  GEOMETRIC_REPRESENTATION_ITEM ( )  RATIONAL_B_SPLINE_CURVE ( ( 1.000000000000000000, 0.9981116584018941973, 0.9981116584018941973, 1.000000000000000000 ) ) 
 REPRESENTATION_ITEM ( '' )  );
#26480=VECTOR ( 'NONE', #117934, 1000.000000000000000 ) ;
#26483=VERTEX_POINT ( 'NONE', #54359 ) ;
#26485=VECTOR ( 'NONE', #106380, 999.9999999999998863 ) ;
#26486=VERTEX_POINT ( 'NONE', #119543 ) ;
#26488=ORIENTED_EDGE ( 'NONE', *, *, #90691, .F. ) ;
#26489=FACE_OUTER_BOUND ( 'NONE', #99717, .T. ) ;
#26490=EDGE_CURVE ( 'NONE', #136986, #6450, #20240, .T. ) ;
#26491=LINE ( 'NONE', #83758, #19145 ) ;
#26492=EDGE_CURVE ( 'NONE', #106952, #81979, #66638, .T. ) ;
#26493=ADVANCED_FACE ( 'NONE', ( #123885 ), #47767, .F. ) ;
#26495=CARTESIAN_POINT ( 'NONE',  ( 27.79289321881327268, -2.240707523384252386, 5.000000000000000000 ) ) ;
#26496=ORIENTED_EDGE ( 'NONE', *, *, #27124, .F. ) ;
#26497=LINE ( 'NONE', #28655, #140984 ) ;
#26499=CARTESIAN_POINT ( 'NONE',  ( -42.18398860626899705, 28.73617430169816700, 5.000000000000000000 ) ) ;
#26500=DIRECTION ( 'NONE',  ( 0.7071067811865487940, 0.7071067811865463515, -0.000000000000000000 ) ) ;
#26501=FACE_OUTER_BOUND ( 'NONE', #81657, .T. ) ;
#26503=LINE ( 'NONE', #16302, #125515 ) ;
#26505=EDGE_CURVE ( 'NONE', #123992, #4634, #68104, .T. ) ;
#26506=CARTESIAN_POINT ( 'NONE',  ( 34.42499999999998295, -1.458600742197942779, 5.000000000000000000 ) ) ;
#26507=CARTESIAN_POINT ( 'NONE',  ( -57.18398860626899705, 28.73617430169827358, 5.000000000000000000 ) ) ;
#26508=ORIENTED_EDGE ( 'NONE', *, *, #119460, .F. ) ;
#26509=ORIENTED_EDGE ( 'NONE', *, *, #114974, .F. ) ;
#26511=EDGE_CURVE ( 'NONE', #103184, #104580, #115082, .T. ) ;
#26512=ORIENTED_EDGE ( 'NONE', *, *, #143247, .T. ) ;
#26514=ORIENTED_EDGE ( 'NONE', *, *, #141793, .F. ) ;
#26515=EDGE_CURVE ( 'NONE', #108363, #141564, #102838, .T. ) ;
#26518=EDGE_CURVE ( 'NONE', #125176, #7159, #134772, .T. ) ;
#26519=ORIENTED_EDGE ( 'NONE', *, *, #69908, .F. ) ;
#26520=LINE ( 'NONE', #57747, #57266 ) ;
#26522=CARTESIAN_POINT ( 'NONE',  ( 48.18398860626899705, 28.73617430169820608, 5.000000000000000000 ) ) ;
#26524=EDGE_CURVE ( 'NONE', #75364, #84656, #49178, .T. ) ;
#26525=LINE ( 'NONE', #80914, #135059 ) ;
#26526=VERTEX_POINT ( 'NONE', #112287 ) ;
#26528=VECTOR ( 'NONE', #114564, 999.9999999999998863 ) ;
#26529=DIRECTION ( 'NONE',  ( -0.6830127018922181881, 0.6830127018922202975, -0.2588190451025214056 ) ) ;
#26530=FACE_OUTER_BOUND ( 'NONE', #124595, .T. ) ;
#26531=VERTEX_POINT ( 'NONE', #4883 ) ;
#26532=DIRECTION ( 'NONE',  ( 0.7071067811865487940, -0.7071067811865463515, 0.000000000000000000 ) ) ;
#26533=EDGE_LOOP ( 'NONE', ( #48639, #61342, #130404, #65510 ) ) ;
#26534=ORIENTED_EDGE ( 'NONE', *, *, #65702, .T. ) ;
#26535=ORIENTED_EDGE ( 'NONE', *, *, #15479, .T. ) ;
#26536=ORIENTED_EDGE ( 'NONE', *, *, #82912, .F. ) ;
#26537=CARTESIAN_POINT ( 'NONE',  ( 33.48921356237309510, -27.52281430457078670, 5.000000000000000000 ) ) ;
#26538=LINE ( 'NONE', #68638, #60769 ) ;
#26539=PLANE ( 'NONE',  #107498 ) ;
#26540=LINE ( 'NONE', #117791, #32098 ) ;
#26541=DIRECTION ( 'NONE',  ( -0.7071067811865486830, -0.7071067811865464625, -0.000000000000000000 ) ) ;
#26542=ORIENTED_EDGE ( 'NONE', *, *, #106820, .T. ) ;
#26543=VECTOR ( 'NONE', #4505, 1000.000000000000000 ) ;
#26544=LINE ( 'NONE', #138167, #3094 ) ;
#26545=EDGE_CURVE ( 'NONE', #130094, #79859, #81088, .T. ) ;
#26546=EDGE_CURVE ( 'NONE', #13632, #94354, #69505, .T. ) ;
#26550=DIRECTION ( 'NONE',  ( -0.7071067811865487940, 0.7071067811865463515, 0.000000000000000000 ) ) ;
#26551=CARTESIAN_POINT ( 'NONE',  ( 31.17183060077625711, -11.24070752338416490, 4.000000000000000000 ) ) ;
#26552=ORIENTED_EDGE ( 'NONE', *, *, #116552, .T. ) ;
#26553=AXIS2_PLACEMENT_3D ( 'NONE', #32121, #87925, #45881 ) ;
#26554=EDGE_LOOP ( 'NONE', ( #41139, #107211, #54506, #113254 ) ) ;
#26555=ORIENTED_EDGE ( 'NONE', *, *, #82349, .F. ) ;
#26556=DIRECTION ( 'NONE',  ( 0.7071067811865487940, 0.7071067811865463515, 0.000000000000000000 ) ) ;
#26557=CARTESIAN_POINT ( 'NONE',  ( 45.18398860626900415, 28.73617430169818832, 5.000000000000000000 ) ) ;
#26558=FACE_OUTER_BOUND ( 'NONE', #6866, .T. ) ;
#26560=EDGE_CURVE ( 'NONE', #139534, #109138, #59906, .T. ) ;
#26564=LINE ( 'NONE', #37454, #57671 ) ;
#26565=VECTOR ( 'NONE', #84530, 1000.000000000000000 ) ;
#26566=DIRECTION ( 'NONE',  ( -0.7071067811865486830, -0.7071067811865464625, 0.000000000000000000 ) ) ;
#26567=DIRECTION ( 'NONE',  ( 0.6830127018922180770, -0.6830127018922204085, -0.2588190451025213501 ) ) ;
#26568=CARTESIAN_POINT ( 'NONE',  ( 13.27644930412397350, 4.689949953678146599, 5.000000000000000000 ) ) ;
#26569=ORIENTED_EDGE ( 'NONE', *, *, #105201, .F. ) ;
#26570=PLANE ( 'NONE',  #80032 ) ;
#26571=ORIENTED_EDGE ( 'NONE', *, *, #33444, .F. ) ;
#26572=DIRECTION ( 'NONE',  ( 0.7071067811865486830, -0.7071067811865464625, -0.000000000000000000 ) ) ;
#26574=VERTEX_POINT ( 'NONE', #136874 ) ;
#26575=CARTESIAN_POINT ( 'NONE',  ( -45.18398860626900415, 28.73617430169818832, 5.000000000000000000 ) ) ;
#26576=CARTESIAN_POINT ( 'NONE',  ( 17.99451991528748351, 28.92564299267950645, 4.000000000000000000 ) ) ;
#26577=ORIENTED_EDGE ( 'NONE', *, *, #129371, .T. ) ;
#26579=ORIENTED_EDGE ( 'NONE', *, *, #92951, .F. ) ;
#26581=ORIENTED_EDGE ( 'NONE', *, *, #143517, .T. ) ;
#26582=CARTESIAN_POINT ( 'NONE',  ( 19.49999999999986500, -7.420205493532880503, -2.617629953481207750 ) ) ;
#26585=CARTESIAN_POINT ( 'NONE',  ( -21.48921356237309155, -27.52281430457070499, 5.000000000000000000 ) ) ;
#26587=VECTOR ( 'NONE', #51315, 1000.000000000000227 ) ;
#26588=CARTESIAN_POINT ( 'NONE',  ( 24.18398860626899705, 28.73617430169804265, 5.000000000000000000 ) ) ;
#26591=CARTESIAN_POINT ( 'NONE',  ( 21.48921356237309155, -27.52281430457070499, 5.000000000000000000 ) ) ;
#26592=LINE ( 'NONE', #106072, #130579 ) ;
#26593=EDGE_CURVE ( 'NONE', #95607, #70988, #113693, .T. ) ;
#26594=CARTESIAN_POINT ( 'NONE',  ( 30.70710678118633297, 17.25929247661554200, 5.000000000000000000 ) ) ;
#26597=DIRECTION ( 'NONE',  ( 0.7071067811865487940, 0.7071067811865463515, 0.000000000000000000 ) ) ;
#26598=VERTEX_POINT ( 'NONE', #114406 ) ;
#26599=DIRECTION ( 'NONE',  ( -0.3543493200069162685, -0.000000000000000000, -0.9351131265310288487 ) ) ;
#26602=LINE ( 'NONE', #135392, #26924 ) ;
#26604=FACE_OUTER_BOUND ( 'NONE', #17881, .T. ) ;
#26605=ORIENTED_EDGE ( 'NONE', *, *, #96670, .T. ) ;
#26606=CARTESIAN_POINT ( 'NONE',  ( 57.48921356237308800, -27.52281430457095368, 5.000000000000000000 ) ) ;
#26607=EDGE_CURVE ( 'NONE', #98525, #36255, #93372, .T. ) ;
#26608=CARTESIAN_POINT ( 'NONE',  ( 8.306730066903963206, -3.740707523384244837, 12.88036043432865618 ) ) ;
#26609=FACE_OUTER_BOUND ( 'NONE', #106654, .T. ) ;
#26611=LINE ( 'NONE', #124494, #68047 ) ;
#26612=DIRECTION ( 'NONE',  ( -0.7071067811865487940, 0.7071067811865463515, 0.000000000000000000 ) ) ;
#26613=VERTEX_POINT ( 'NONE', #46342 ) ;
#26614=CARTESIAN_POINT ( 'NONE',  ( 29.99999999999980105, -19.06887692260762179, 4.000000000000000000 ) ) ;
#26615=PLANE ( 'NONE',  #43056 ) ;
#26617=CARTESIAN_POINT ( 'NONE',  ( -23.20710678118638270, -17.24070752338409918, 5.000000000000000000 ) ) ;
#26618=ADVANCED_FACE ( 'NONE', ( #3480 ), #25982, .F. ) ;
#26619=EDGE_CURVE ( 'NONE', #93975, #84503, #81822, .T. ) ;
#26620=ORIENTED_EDGE ( 'NONE', *, *, #132303, .T. ) ;
#26621=ORIENTED_EDGE ( 'NONE', *, *, #70605, .T. ) ;
#26622=ORIENTED_EDGE ( 'NONE', *, *, #98178, .T. ) ;
#26624=EDGE_LOOP ( 'NONE', ( #9368, #2797, #124159, #131159 ) ) ;
#26625=ADVANCED_FACE ( 'NONE', ( #90530 ), #35463, .F. ) ;
#26626=CARTESIAN_POINT ( 'NONE',  ( 17.99999999999987566, 12.25461709320621928, -10.07315571508693175 ) ) ;
#26627=LINE ( 'NONE', #38931, #80453 ) ;
#26628=LINE ( 'NONE', #104896, #110476 ) ;
#26629=DIRECTION ( 'NONE',  ( -0.6830127018922181881, 0.6830127018922202975, -0.2588190451025214056 ) ) ;
#26630=ORIENTED_EDGE ( 'NONE', *, *, #81250, .F. ) ;
#26631=CARTESIAN_POINT ( 'NONE',  ( 5.510786437626906675, -27.52281430457051314, 5.000000000000000000 ) ) ;
#26635=VERTEX_POINT ( 'NONE', #10447 ) ;
#26636=PLANE ( 'NONE',  #97554 ) ;
#26637=CARTESIAN_POINT ( 'NONE',  ( -9.005480084712511157, 28.92564299267931816, 4.000000000000000000 ) ) ;
#26638=DIRECTION ( 'NONE',  ( -0.7071067811865486830, -0.7071067811865464625, -0.000000000000000000 ) ) ;
#26640=ORIENTED_EDGE ( 'NONE', *, *, #57950, .T. ) ;
#26641=ORIENTED_EDGE ( 'NONE', *, *, #90268, .F. ) ;
#26642=CARTESIAN_POINT ( 'NONE',  ( -54.48921356237310221, -27.52281430457093236, 5.000000000000000000 ) ) ;
#26643=CARTESIAN_POINT ( 'NONE',  ( -57.48921356237308800, -27.52281430457095368, 5.000000000000000000 ) ) ;
#26644=CARTESIAN_POINT ( 'NONE',  ( -9.299744871391588674, -27.71228299555212971, 4.000000000000000000 ) ) ;
#26647=CARTESIAN_POINT ( 'NONE',  ( -34.45011844616454511, -14.99769585840588704, 5.000000000000000888 ) ) ;
#26648=PLANE ( 'NONE',  #129877 ) ;
#26652=ORIENTED_EDGE ( 'NONE', *, *, #119415, .F. ) ;
#26654=CARTESIAN_POINT ( 'NONE',  ( -28.49999999999980105, 10.08746187583914988, 4.000000000000000000 ) ) ;
#26655=EDGE_LOOP ( 'NONE', ( #101686, #43074, #100856, #75227 ) ) ;
#26656=EDGE_CURVE ( 'NONE', #52412, #57071, #142428, .T. ) ;
#26657=CARTESIAN_POINT ( 'NONE',  ( -0.2997448713915885632, -27.71228299555206220, 4.000000000000000000 ) ) ;
#26658=EDGE_CURVE ( 'NONE', #70384, #71407, #109777, .T. ) ;
#26659=CARTESIAN_POINT ( 'NONE',  ( -24.29974487139158867, -27.71228299555223273, 4.000000000000000000 ) ) ;
#26660=VERTEX_POINT ( 'NONE', #141710 ) ;
#26663=PLANE ( 'NONE',  #139768 ) ;
#26664=EDGE_CURVE ( 'NONE', #27623, #136020, #64866, .T. ) ;
#26665=CARTESIAN_POINT ( 'NONE',  ( -34.92500000000001137, 17.81665438641024579, 4.500000000000000888 ) ) ;
#26666=PLANE ( 'NONE',  #28235 ) ;
#26667=ORIENTED_EDGE ( 'NONE', *, *, #54325, .T. ) ;
#26668=EDGE_CURVE ( 'NONE', #34776, #26933, #9736, .T. ) ;
#26669=CARTESIAN_POINT ( 'NONE',  ( 0.000000000000000000, 0.000000000000000000, 5.000000000000000000 ) ) ;
#26670=PLANE ( 'NONE',  #134492 ) ;
#26671=VERTEX_POINT ( 'NONE', #74315 ) ;
#26672=LINE ( 'NONE', #51298, #13296 ) ;
#26673=ORIENTED_EDGE ( 'NONE', *, *, #93291, .F. ) ;
#26674=ORIENTED_EDGE ( 'NONE', *, *, #78642, .F. ) ;
#26675=FACE_OUTER_BOUND ( 'NONE', #115994, .T. ) ;
#26676=ORIENTED_EDGE ( 'NONE', *, *, #34925, .T. ) ;
#26679=ORIENTED_EDGE ( 'NONE', *, *, #119579, .T. ) ;
#26682=VECTOR ( 'NONE', #104046, 1000.000000000000000 ) ;
#26686=LINE ( 'NONE', #83957, #91116 ) ;
#26687=AXIS2_PLACEMENT_3D ( 'NONE', #73527, #98129, #62649 ) ;
#26688=EDGE_CURVE ( 'NONE', #138855, #115521, #18449, .T. ) ;
#26690=DIRECTION ( 'NONE',  ( 1.000000000000000000, 0.000000000000000000, 0.000000000000000000 ) ) ;
#26693=ADVANCED_FACE ( 'NONE', ( #21348 ), #51848, .F. ) ;
#26694=PLANE ( 'NONE',  #90958 ) ;
#26697=VERTEX_POINT ( 'NONE', #119907 ) ;
#26698=DIRECTION ( 'NONE',  ( 0.6830127018922181881, 0.6830127018922202975, -0.2588190451025214056 ) ) ;
#26699=DIRECTION ( 'NONE',  ( -0.7071067811865486830, -0.7071067811865464625, 0.000000000000000000 ) ) ;
#26700=ORIENTED_EDGE ( 'NONE', *, *, #79862, .F. ) ;
#26701=EDGE_LOOP ( 'NONE', ( #100008, #16552, #128053, #87826 ) ) ;
#26702=LINE ( 'NONE', #25263, #79641 ) ;
#26703=ORIENTED_EDGE ( 'NONE', *, *, #96171, .T. ) ;
#26704=CARTESIAN_POINT ( 'NONE',  ( -0.4892135623730947680, -27.52281430457055578, 5.000000000000000000 ) ) ;
#26706=LINE ( 'NONE', #59369, #5 ) ;
#26708=VERTEX_POINT ( 'NONE', #96036 ) ;
#26709=CARTESIAN_POINT ( 'NONE',  ( 45.29974487139158867, -27.71228299555237840, 4.000000000000000000 ) ) ;
#26711=CARTESIAN_POINT ( 'NONE',  ( -11.24139925780195171, 21.72500000000000142, 5.000000000000000000 ) ) ;
#26713=CARTESIAN_POINT ( 'NONE',  ( 12.18398860626900060, 28.73617430169795739, 5.000000000000000000 ) ) ;
#26714=CARTESIAN_POINT ( 'NONE',  ( -27.29974487139158512, -27.71228299555225405, 4.000000000000000000 ) ) ;
#26716=ORIENTED_EDGE ( 'NONE', *, *, #133281, .T. ) ;
#26717=ORIENTED_EDGE ( 'NONE', *, *, #31581, .T. ) ;
#26718=ORIENTED_EDGE ( 'NONE', *, *, #13230, .T. ) ;
#26719=CARTESIAN_POINT ( 'NONE',  ( -34.92190055902135271, 21.78725130426367684, 4.173570450635298634 ) ) ;
#26720=DIRECTION ( 'NONE',  ( 0.7071067811865486830, -0.7071067811865464625, -0.000000000000000000 ) ) ;
#26721=CARTESIAN_POINT ( 'NONE',  ( 5.700255128608413102, -27.71228299555201957, 4.000000000000000000 ) ) ;
#26722=PLANE ( 'NONE',  #51938 ) ;
#26723=ORIENTED_EDGE ( 'NONE', *, *, #62050, .T. ) ;
#26724=EDGE_CURVE ( 'NONE', #119189, #35816, #32226, .T. ) ;
#26725=DIRECTION ( 'NONE',  ( 0.7071067811865487940, -0.7071067811865463515, 0.000000000000000000 ) ) ;
#26726=LINE ( 'NONE', #128200, #61926 ) ;
#26727=DIRECTION ( 'NONE',  ( 0.7071067811865486830, -0.7071067811865464625, -0.000000000000000000 ) ) ;
#26728=CARTESIAN_POINT ( 'NONE',  ( 51.18398860626899705, 28.73617430169823095, 5.000000000000000000 ) ) ;
#26729=CARTESIAN_POINT ( 'NONE',  ( 33.79289321881323360, -14.24070752338413648, 5.000000000000000000 ) ) ;
#26732=LINE ( 'NONE', #73123, #26224 ) ;
#26734=( BOUNDED_CURVE ( )  B_SPLINE_CURVE ( 3, ( #344, #77257, #133058, #78653 ),
 .UNSPECIFIED., .F., .F. ) 
 B_SPLINE_CURVE_WITH_KNOTS ( ( 4, 4 ),
 ( 1.208578181583235267, 1.359146454359428269 ),
 .UNSPECIFIED. ) 
 CURVE ( )  GEOMETRIC_REPRESENTATION_ITEM ( )  RATIONAL_B_SPLINE_CURVE ( ( 1.000000000000000000, 0.9981116584018955296, 0.9981116584018955296, 1.000000000000000000 ) ) 
 REPRESENTATION_ITEM ( '' )  );
#26737=ORIENTED_EDGE ( 'NONE', *, *, #70300, .F. ) ;
#26738=EDGE_LOOP ( 'NONE', ( #63267, #95274, #106220, #77347 ) ) ;
#26739=LINE ( 'NONE', #105698, #137172 ) ;
#26740=CARTESIAN_POINT ( 'NONE',  ( 18.18398860626898994, 28.73617430169800002, 5.000000000000000000 ) ) ;
#26741=LINE ( 'NONE', #16559, #34548 ) ;
#26743=FACE_OUTER_BOUND ( 'NONE', #20955, .T. ) ;
#26744=EDGE_LOOP ( 'NONE', ( #107444, #28205, #50023, #68837, #44312, #41450 ) ) ;
#26745=DIRECTION ( 'NONE',  ( -0.7071067811865486830, -0.7071067811865464625, 0.000000000000000000 ) ) ;
#26746=CARTESIAN_POINT ( 'NONE',  ( -48.18398860626899705, 28.73617430169820608, 5.000000000000000000 ) ) ;
#26747=AXIS2_PLACEMENT_3D ( 'NONE', #20716, #141818, #100441 ) ;
#26749=FACE_OUTER_BOUND ( 'NONE', #71331, .T. ) ;
#26750=FACE_OUTER_BOUND ( 'NONE', #51842, .T. ) ;
#26751=VECTOR ( 'NONE', #109175, 1000.000000000000000 ) ;
#26752=PLANE ( 'NONE',  #46844 ) ;
#26753=LINE ( 'NONE', #49255, #68000 ) ;
#26758=CARTESIAN_POINT ( 'NONE',  ( 28.82816939922332011, 3.759292476615674783, 4.000000000000000000 ) ) ;
#26759=LINE ( 'NONE', #113041, #1410 ) ;
#26760=ORIENTED_EDGE ( 'NONE', *, *, #24964, .T. ) ;
#26763=ORIENTED_EDGE ( 'NONE', *, *, #49739, .F. ) ;
#26764=VECTOR ( 'NONE', #55657, 1000.000000000000000 ) ;
#26766=EDGE_CURVE ( 'NONE', #139864, #132371, #109047, .T. ) ;
#26767=DIRECTION ( 'NONE',  ( -0.000000000000000000, -0.3543493200069152693, 0.9351131265310292928 ) ) ;
#26768=CARTESIAN_POINT ( 'NONE',  ( 60.29974487139158867, -27.71228299555248142, 4.000000000000000000 ) ) ;
#26769=CARTESIAN_POINT ( 'NONE',  ( 33.18398860626899705, 28.73617430169810305, 5.000000000000000000 ) ) ;
#26770=VERTEX_POINT ( 'NONE', #30819 ) ;
#26771=CARTESIAN_POINT ( 'NONE',  ( 54.18398860626899705, 28.73617430169825226, 5.000000000000000000 ) ) ;
#26772=FACE_OUTER_BOUND ( 'NONE', #42421, .T. ) ;
#26773=CARTESIAN_POINT ( 'NONE',  ( -30.48921356237309510, -27.52281430457076894, 5.000000000000000000 ) ) ;
#26775=ADVANCED_FACE ( 'NONE', ( #19204 ), #115792, .T. ) ;
#26777=CARTESIAN_POINT ( 'NONE',  ( 0.000000000000000000, 0.000000000000000000, 5.000000000000000000 ) ) ;
#26781=DIRECTION ( 'NONE',  ( -0.000000000000000000, 0.3543493200069153248, 0.9351131265310292928 ) ) ;
#26783=FACE_OUTER_BOUND ( 'NONE', #71848, .T. ) ;
#26784=VECTOR ( 'NONE', #120009, 1000.000000000000000 ) ;
#26787=EDGE_CURVE ( 'NONE', #23165, #50701, #124225, .T. ) ;
#26788=VERTEX_POINT ( 'NONE', #99593 ) ;
#26789=ORIENTED_EDGE ( 'NONE', *, *, #22690, .T. ) ;
#26790=VECTOR ( 'NONE', #73172, 1000.000000000000000 ) ;
#26792=ORIENTED_EDGE ( 'NONE', *, *, #85085, .T. ) ;
#26793=AXIS2_PLACEMENT_3D ( 'NONE', #100700, #36164, #1346 ) ;
#26794=EDGE_CURVE ( 'NONE', #12163, #5176, #34368, .T. ) ;
#26795=VECTOR ( 'NONE', #88268, 1000.000000000000000 ) ;
#26796=EDGE_CURVE ( 'NONE', #25077, #86768, #46729, .T. ) ;
#26797=LINE ( 'NONE', #135582, #131092 ) ;
#26798=ORIENTED_EDGE ( 'NONE', *, *, #11382, .F. ) ;
#26799=LINE ( 'NONE', #24652, #137020 ) ;
#26800=CARTESIAN_POINT ( 'NONE',  ( -42.48921356237308800, -27.52281430457085065, 5.000000000000000000 ) ) ;
#26801=EDGE_CURVE ( 'NONE', #32049, #2079, #24901, .T. ) ;
#26803=VERTEX_POINT ( 'NONE', #88033 ) ;
#26804=ORIENTED_EDGE ( 'NONE', *, *, #66937, .F. ) ;
#26805=CARTESIAN_POINT ( 'NONE',  ( 57.18398860626899705, 28.73617430169827358, 5.000000000000000000 ) ) ;
#26806=CARTESIAN_POINT ( 'NONE',  ( -24.66331758004193375, 1.142935889642021863, 4.329525704382053419 ) ) ;
#26807=ADVANCED_FACE ( 'NONE', ( #13295 ), #101755, .F. ) ;
#26808=VERTEX_POINT ( 'NONE', #56159 ) ;
#26810=ORIENTED_EDGE ( 'NONE', *, *, #76425, .F. ) ;
#26812=ADVANCED_FACE ( 'NONE', ( #113330 ), #14012, .F. ) ;
#26813=PLANE ( 'NONE',  #64138 ) ;
#26816=ORIENTED_EDGE ( 'NONE', *, *, #135980, .F. ) ;
#26817=VERTEX_POINT ( 'NONE', #143121 ) ;
#26818=DIRECTION ( 'NONE',  ( -0.3543493200069162685, -0.000000000000000000, -0.9351131265310288487 ) ) ;
#26819=ORIENTED_EDGE ( 'NONE', *, *, #44118, .T. ) ;
#26820=ORIENTED_EDGE ( 'NONE', *, *, #31283, .F. ) ;
#26821=EDGE_CURVE ( 'NONE', #41198, #33680, #43815, .T. ) ;
#26822=DIRECTION ( 'NONE',  ( -0.000000000000000000, -0.000000000000000000, 1.000000000000000000 ) ) ;
#26823=EDGE_CURVE ( 'NONE', #62376, #35148, #24208, .T. ) ;
#26824=FACE_OUTER_BOUND ( 'NONE', #51193, .T. ) ;
#26825=ORIENTED_EDGE ( 'NONE', *, *, #142710, .F. ) ;
#26826=LINE ( 'NONE', #94921, #20525 ) ;
#26828=DIRECTION ( 'NONE',  ( 0.6830127018922180770, -0.6830127018922204085, -0.2588190451025213501 ) ) ;
#26829=LINE ( 'NONE', #124017, #103929 ) ;
#26830=EDGE_CURVE ( 'NONE', #24642, #50272, #122798, .T. ) ;
#26831=EDGE_CURVE ( 'NONE', #136190, #75148, #121357, .T. ) ;
#26832=CARTESIAN_POINT ( 'NONE',  ( 24.18398860626899705, 28.73617430169804265, 5.000000000000000000 ) ) ;
#26833=FACE_BOUND ( 'NONE', #90542, .T. ) ;
#26836=DIRECTION ( 'NONE',  ( -0.000000000000000000, -0.3543493200069152693, 0.9351131265310292928 ) ) ;
#26837=DIRECTION ( 'NONE',  ( 0.7071067811865487940, 0.7071067811865463515, -0.000000000000000000 ) ) ;
#26838=ORIENTED_EDGE ( 'NONE', *, *, #68388, .T. ) ;
#26839=DIRECTION ( 'NONE',  ( 0.7071067811865487940, 0.7071067811865463515, -0.000000000000000000 ) ) ;
#26841=ORIENTED_EDGE ( 'NONE', *, *, #19138, .F. ) ;
#26842=EDGE_LOOP ( 'NONE', ( #57581, #124651, #17644, #16651 ) ) ;
#26845=VERTEX_POINT ( 'NONE', #11870 ) ;
#26847=VECTOR ( 'NONE', #63403, 1000.000000000000000 ) ;
#26848=CARTESIAN_POINT ( 'NONE',  ( 42.29974487139158157, -27.71228299555235708, 4.000000000000000000 ) ) ;
#26849=LINE ( 'NONE', #129015, #114472 ) ;
#26850=EDGE_CURVE ( 'NONE', #29147, #19199, #994, .T. ) ;
#26851=EDGE_LOOP ( 'NONE', ( #66549, #14049, #90546, #45496 ) ) ;
#26854=LINE ( 'NONE', #103673, #118659 ) ;
#26855=DIRECTION ( 'NONE',  ( -0.7071067811865486830, -0.7071067811865464625, 0.000000000000000000 ) ) ;
#26857=LINE ( 'NONE', #71110, #115412 ) ;
#26858=EDGE_CURVE ( 'NONE', #38224, #65695, #23480, .T. ) ;
#26859=PLANE ( 'NONE',  #17017 ) ;
#26861=ORIENTED_EDGE ( 'NONE', *, *, #140373, .T. ) ;
#26862=ORIENTED_EDGE ( 'NONE', *, *, #128865, .F. ) ;
#26866=ORIENTED_EDGE ( 'NONE', *, *, #121312, .F. ) ;
#26867=ORIENTED_EDGE ( 'NONE', *, *, #130276, .F. ) ;
#26868=CARTESIAN_POINT ( 'NONE',  ( -21.00548008471250938, 28.92564299267923644, 4.000000000000000000 ) ) ;
#26869=CARTESIAN_POINT ( 'NONE',  ( -26.20710678118635428, -14.24070752338413470, 5.000000000000000000 ) ) ;
#26870=ADVANCED_FACE ( 'NONE', ( #111938 ), #68457, .F. ) ;
#26871=CARTESIAN_POINT ( 'NONE',  ( -42.18398860626899705, 28.73617430169816700, 5.000000000000000000 ) ) ;
#26872=VERTEX_POINT ( 'NONE', #90160 ) ;
#26874=VERTEX_POINT ( 'NONE', #134407 ) ;
#26877=ADVANCED_FACE ( 'NONE', ( #35105 ), #123545, .T. ) ;
#26878=DIRECTION ( 'NONE',  ( -0.000000000000000000, 0.3543493200069153248, 0.9351131265310292928 ) ) ;
#26879=VECTOR ( 'NONE', #103118, 999.9999999999998863 ) ;
#26881=EDGE_LOOP ( 'NONE', ( #74389, #124238, #35248, #68453 ) ) ;
#26883=LINE ( 'NONE', #104433, #112476 ) ;
#26884=VECTOR ( 'NONE', #34114, 999.9999999999998863 ) ;
#26886=LINE ( 'NONE', #138515, #99788 ) ;
#26887=ORIENTED_EDGE ( 'NONE', *, *, #41052, .F. ) ;
#26889=CARTESIAN_POINT ( 'NONE',  ( 51.18398860626899705, 28.73617430169823095, 5.000000000000000000 ) ) ;
#26890=ORIENTED_EDGE ( 'NONE', *, *, #77740, .T. ) ;
#26892=CARTESIAN_POINT ( 'NONE',  ( -2.292986735706930457, -21.74070752338405299, 4.999753212805217117 ) ) ;
#26894=CARTESIAN_POINT ( 'NONE',  ( -32.99999999999976552, 17.58746187583906462, 4.000000000000000000 ) ) ;
#26895=FACE_OUTER_BOUND ( 'NONE', #4936, .T. ) ;
#26896=FACE_OUTER_BOUND ( 'NONE', #82955, .T. ) ;
#26898=ORIENTED_EDGE ( 'NONE', *, *, #34872, .T. ) ;
#26899=EDGE_CURVE ( 'NONE', #100056, #76924, #127071, .T. ) ;
#26900=LINE ( 'NONE', #7254, #34416 ) ;
#26902=LINE ( 'NONE', #60274, #134604 ) ;
#26903=CARTESIAN_POINT ( 'NONE',  ( -15.29974487139158867, -27.71228299555216879, 4.000000000000000000 ) ) ;
#26904=VERTEX_POINT ( 'NONE', #50249 ) ;
#26905=CARTESIAN_POINT ( 'NONE',  ( 5.994519915287488843, 28.92564299267942118, 4.000000000000000000 ) ) ;
#26906=DIRECTION ( 'NONE',  ( 0.7071067811865487940, 0.7071067811865463515, -0.000000000000000000 ) ) ;
#26907=ORIENTED_EDGE ( 'NONE', *, *, #34068, .F. ) ;
#26908=DIRECTION ( 'NONE',  ( -0.6830127018922180770, -0.6830127018922202975, -0.2588190451025213501 ) ) ;
#26909=EDGE_LOOP ( 'NONE', ( #38254, #5721, #132158, #130865 ) ) ;
#26910=EDGE_CURVE ( 'NONE', #91471, #99307, #127815, .T. ) ;
#26914=ORIENTED_EDGE ( 'NONE', *, *, #46115, .F. ) ;
#26918=ORIENTED_EDGE ( 'NONE', *, *, #27761, .F. ) ;
#26919=LINE ( 'NONE', #98939, #50813 ) ;
#26921=DIRECTION ( 'NONE',  ( 0.7071067811865486830, -0.7071067811865464625, -0.000000000000000000 ) ) ;
#26923=DIRECTION ( 'NONE',  ( -0.000000000000000000, 0.3543493200069153248, 0.9351131265310292928 ) ) ;
#26924=VECTOR ( 'NONE', #3393, 1000.000000000000000 ) ;
#26925=FACE_OUTER_BOUND ( 'NONE', #6271, .T. ) ;
#26926=CARTESIAN_POINT ( 'NONE',  ( -34.92500000000001137, 4.701930566820959001, 4.500000000000000888 ) ) ;
#26929=EDGE_LOOP ( 'NONE', ( #76494, #119941, #131558, #46333 ) ) ;
#26932=ORIENTED_EDGE ( 'NONE', *, *, #27303, .F. ) ;
#26933=VERTEX_POINT ( 'NONE', #137257 ) ;
#26934=ORIENTED_EDGE ( 'NONE', *, *, #39987, .T. ) ;
#26935=CIRCLE ( 'NONE', #8469, 0.5000000000000004441 ) ;
#26937=LINE ( 'NONE', #28384, #104150 ) ;
#26938=ORIENTED_EDGE ( 'NONE', *, *, #131035, .F. ) ;
#26939=CARTESIAN_POINT ( 'NONE',  ( 10.49999999999993427, 1.466399257802251999, 5.000000000000000000 ) ) ;
#26940=DIRECTION ( 'NONE',  ( 0.000000000000000000, 1.000000000000000000, 0.000000000000000000 ) ) ;
#26941=LINE ( 'NONE', #3041, #65151 ) ;
#26943=ORIENTED_EDGE ( 'NONE', *, *, #45322, .F. ) ;
#26947=CARTESIAN_POINT ( 'NONE',  ( 14.99999999999989519, -8.731860332648830436, -2.120594902707502616 ) ) ;
#26948=DIRECTION ( 'NONE',  ( 0.7071067811865486830, -0.7071067811865464625, -0.000000000000000000 ) ) ;
#26949=FACE_OUTER_BOUND ( 'NONE', #134091, .T. ) ;
#26950=CARTESIAN_POINT ( 'NONE',  ( 8.292893218813400580, 5.259292476615665457, 5.000000000000000000 ) ) ;
#26953=DIRECTION ( 'NONE',  ( -0.6830127018922181881, 0.6830127018922202975, -0.2588190451025214056 ) ) ;
#26954=ADVANCED_FACE ( 'NONE', ( #83603 ), #135820, .T. ) ;
#26955=ORIENTED_EDGE ( 'NONE', *, *, #104183, .F. ) ;
#26956=ORIENTED_EDGE ( 'NONE', *, *, #97633, .T. ) ;
#26958=EDGE_CURVE ( 'NONE', #17934, #86656, #71293, .T. ) ;
#26959=EDGE_LOOP ( 'NONE', ( #63870, #104094, #48901, #6639 ) ) ;
#26960=ORIENTED_EDGE ( 'NONE', *, *, #5057, .F. ) ;
#26961=CARTESIAN_POINT ( 'NONE',  ( -34.17183060077623225, 6.759292476615649470, 4.000000000000000000 ) ) ;
#26962=ADVANCED_FACE ( 'NONE', ( #72026 ), #104609, .F. ) ;
#26964=VERTEX_POINT ( 'NONE', #17583 ) ;
#26966=DIRECTION ( 'NONE',  ( 0.7071067811865487940, 0.7071067811865463515, -0.000000000000000000 ) ) ;
#26968=CARTESIAN_POINT ( 'NONE',  ( -13.99806943317891772, -22.22500000000000142, 4.500000000000000888 ) ) ;
#26970=AXIS2_PLACEMENT_3D ( 'NONE', #51991, #104926, #17883 ) ;
#26971=ORIENTED_EDGE ( 'NONE', *, *, #73533, .F. ) ;
#26972=EDGE_CURVE ( 'NONE', #79253, #14518, #5273, .T. ) ;
#26973=CARTESIAN_POINT ( 'NONE',  ( -12.48921356237309155, -27.52281430457064104, 5.000000000000000000 ) ) ;
#26974=ORIENTED_EDGE ( 'NONE', *, *, #94830, .F. ) ;
#26975=DIRECTION ( 'NONE',  ( 0.3543493200069162685, -0.000000000000000000, -0.9351131265310288487 ) ) ;
#26976=CARTESIAN_POINT ( 'NONE',  ( -25.49999999999981881, 0.05218569542917578241, 5.000000000000000000 ) ) ;
#26977=LINE ( 'NONE', #5202, #46798 ) ;
#26978=EDGE_CURVE ( 'NONE', #118900, #133790, #126358, .T. ) ;
#26979=CARTESIAN_POINT ( 'NONE',  ( 48.48921356237309510, -27.52281430457089328, 5.000000000000000000 ) ) ;
#26981=VECTOR ( 'NONE', #66412, 1000.000000000000000 ) ;
#26982=EDGE_CURVE ( 'NONE', #63812, #111783, #3820, .T. ) ;
#26983=ORIENTED_EDGE ( 'NONE', *, *, #39718, .T. ) ;
#26984=FACE_OUTER_BOUND ( 'NONE', #96100, .T. ) ;
#26985=CARTESIAN_POINT ( 'NONE',  ( 5.821832416544749478, 22.22500000000000142, -10.44049799921112687 ) ) ;
#26986=CARTESIAN_POINT ( 'NONE',  ( 12.48921356237309155, -27.52281430457064104, 5.000000000000000000 ) ) ;
#26987=LINE ( 'NONE', #35041, #99578 ) ;
#26988=EDGE_CURVE ( 'NONE', #138243, #13156, #48107, .T. ) ;
#26991=VECTOR ( 'NONE', #87785, 1000.000000000000000 ) ;
#26993=VERTEX_POINT ( 'NONE', #92290 ) ;
#26994=LINE ( 'NONE', #124883, #85936 ) ;
#26996=VERTEX_POINT ( 'NONE', #136514 ) ;
#26997=ORIENTED_EDGE ( 'NONE', *, *, #46857, .T. ) ;
#26998=VECTOR ( 'NONE', #50654, 1000.000000000000000 ) ;
#26999=CARTESIAN_POINT ( 'NONE',  ( 12.48921356237309155, -27.52281430457064104, 5.000000000000000000 ) ) ;
#27000=VERTEX_POINT ( 'NONE', #61168 ) ;
#27001=DIRECTION ( 'NONE',  ( -0.7071067811865486830, -0.7071067811865464625, -0.000000000000000000 ) ) ;
#27002=VERTEX_POINT ( 'NONE', #59705 ) ;
#27003=CARTESIAN_POINT ( 'NONE',  ( 28.49999999999979750, 15.43112307739202649, 4.000000000000000000 ) ) ;
#27004=EDGE_CURVE ( 'NONE', #94256, #109940, #137971, .T. ) ;
#27005=CARTESIAN_POINT ( 'NONE',  ( -30.48921356237309510, -27.52281430457076894, 5.000000000000000000 ) ) ;
#27007=FACE_BOUND ( 'NONE', #66167, .T. ) ;
#27008=DIRECTION ( 'NONE',  ( -0.000000000000000000, 0.3543493200069153248, 0.9351131265310292928 ) ) ;
#27009=FACE_OUTER_BOUND ( 'NONE', #120235, .T. ) ;
#27010=DIRECTION ( 'NONE',  ( 0.7071067811865487940, 0.7071067811865463515, 0.000000000000000000 ) ) ;
#27011=ORIENTED_EDGE ( 'NONE', *, *, #64744, .T. ) ;
#27012=CARTESIAN_POINT ( 'NONE',  ( 13.49999999999991829, 16.08746187583907883, 4.000000000000000000 ) ) ;
#27014=ORIENTED_EDGE ( 'NONE', *, *, #58594, .F. ) ;
#27015=CARTESIAN_POINT ( 'NONE',  ( -39.18398860626899705, 28.73617430169814568, 5.000000000000000000 ) ) ;
#27016=EDGE_CURVE ( 'NONE', #120012, #14271, #74738, .T. ) ;
#27017=VERTEX_POINT ( 'NONE', #38650 ) ;
#27018=ORIENTED_EDGE ( 'NONE', *, *, #86896, .F. ) ;
#27020=EDGE_LOOP ( 'NONE', ( #32429, #16460, #67252, #94353, #13800, #10745 ) ) ;
#27021=DIRECTION ( 'NONE',  ( 4.681814790819592407E-17, 0.3543493200069153248, 0.9351131265310292928 ) ) ;
#27023=EDGE_CURVE ( 'NONE', #15277, #53474, #59093, .T. ) ;
#27024=ORIENTED_EDGE ( 'NONE', *, *, #128606, .F. ) ;
#27025=FACE_OUTER_BOUND ( 'NONE', #136346, .T. ) ;
#27026=AXIS2_PLACEMENT_3D ( 'NONE', #103617, #126802, #136989 ) ;
#27027=DIRECTION ( 'NONE',  ( -0.7071067811865486830, -0.7071067811865464625, 0.000000000000000000 ) ) ;
#27029=DIRECTION ( 'NONE',  ( 1.000000000000000000, 0.000000000000000000, 0.000000000000000000 ) ) ;
#27030=CARTESIAN_POINT ( 'NONE',  ( 11.99999999999991296, -22.22500000000000853, 4.412002311790018894 ) ) ;
#27031=CARTESIAN_POINT ( 'NONE',  ( 6.489213562373093325, -27.52281430457059841, 5.000000000000000000 ) ) ;
#27032=CARTESIAN_POINT ( 'NONE',  ( -78.29974487139158157, -27.71228299555260577, 4.000000000000000000 ) ) ;
#27033=ORIENTED_EDGE ( 'NONE', *, *, #12222, .T. ) ;
#27034=VECTOR ( 'NONE', #65485, 1000.000000000000227 ) ;
#27035=ORIENTED_EDGE ( 'NONE', *, *, #55103, .T. ) ;
#27036=FACE_OUTER_BOUND ( 'NONE', #126254, .T. ) ;
#27037=FACE_OUTER_BOUND ( 'NONE', #2917, .T. ) ;
#27039=ORIENTED_EDGE ( 'NONE', *, *, #12647, .T. ) ;
#27040=ORIENTED_EDGE ( 'NONE', *, *, #24484, .F. ) ;
#27044=ADVANCED_FACE ( 'NONE', ( #118327 ), #62554, .F. ) ;
#27048=AXIS2_PLACEMENT_3D ( 'NONE', #131345, #118305, #140770 ) ;
#27051=DIRECTION ( 'NONE',  ( 0.7071067811865486830, -0.7071067811865464625, -0.000000000000000000 ) ) ;
#27052=ORIENTED_EDGE ( 'NONE', *, *, #35015, .T. ) ;
#27053=CIRCLE ( 'NONE', #119650, 0.5000000000000004441 ) ;
#27054=LINE ( 'NONE', #50257, #118320 ) ;
#27056=DIRECTION ( 'NONE',  ( -0.7071067811865486830, -0.7071067811865464625, 0.000000000000000000 ) ) ;
#27057=ORIENTED_EDGE ( 'NONE', *, *, #20748, .T. ) ;
#27059=VERTEX_POINT ( 'NONE', #107458 ) ;
#27060=CARTESIAN_POINT ( 'NONE',  ( 35.99451991528749772, 28.92564299267963079, 4.000000000000000000 ) ) ;
#27061=CARTESIAN_POINT ( 'NONE',  ( -6.489213562373093325, -27.52281430457059841, 5.000000000000000000 ) ) ;
#27062=PLANE ( 'NONE',  #72567 ) ;
#27063=ORIENTED_EDGE ( 'NONE', *, *, #98081, .F. ) ;
#27064=LINE ( 'NONE', #117435, #13480 ) ;
#27065=ADVANCED_FACE ( 'NONE', ( #139421 ), #142262, .T. ) ;
#27068=DIRECTION ( 'NONE',  ( 0.7071067811865487940, 0.7071067811865463515, 0.000000000000000000 ) ) ;
#27069=ORIENTED_EDGE ( 'NONE', *, *, #84374, .T. ) ;
#27070=CARTESIAN_POINT ( 'NONE',  ( 0.000000000000000000, 0.000000000000000000, 5.000000000000000000 ) ) ;
#27071=LINE ( 'NONE', #71316, #141982 ) ;
#27073=FACE_OUTER_BOUND ( 'NONE', #44443, .T. ) ;
#27074=VECTOR ( 'NONE', #46301, 1000.000000000000000 ) ;
#27076=ORIENTED_EDGE ( 'NONE', *, *, #37001, .T. ) ;
#27077=EDGE_CURVE ( 'NONE', #42201, #7059, #119737, .T. ) ;
#27078=VERTEX_POINT ( 'NONE', #29890 ) ;
#27079=LINE ( 'NONE', #136548, #54142 ) ;
#27080=LINE ( 'NONE', #106044, #6549 ) ;
#27081=VECTOR ( 'NONE', #122930, 999.9999999999998863 ) ;
#27082=VECTOR ( 'NONE', #140568, 1000.000000000000227 ) ;
#27084=CARTESIAN_POINT ( 'NONE',  ( 34.92499999999998295, -0.1586646689214626926, -3.482007288379075582 ) ) ;
#27085=AXIS2_PLACEMENT_3D ( 'NONE', #31431, #71551, #49095 ) ;
#27086=DIRECTION ( 'NONE',  ( -0.3543493200069162685, -0.000000000000000000, -0.9351131265310288487 ) ) ;
#27087=LINE ( 'NONE', #27805, #80712 ) ;
#27088=PLANE ( 'NONE',  #21357 ) ;
#27089=ORIENTED_EDGE ( 'NONE', *, *, #54485, .F. ) ;
#27090=LINE ( 'NONE', #93072, #18693 ) ;
#27091=VECTOR ( 'NONE', #40534, 1000.000000000000000 ) ;
#27092=CARTESIAN_POINT ( 'NONE',  ( -3.183988606268992161, 28.73617430169789699, 5.000000000000000000 ) ) ;
#27093=AXIS2_PLACEMENT_3D ( 'NONE', #117679, #51769, #140877 ) ;
#27094=CARTESIAN_POINT ( 'NONE',  ( -72.18398860626899705, 28.73617430169837661, 5.000000000000000000 ) ) ;
#27096=ADVANCED_FACE ( 'NONE', ( #74134 ), #40110, .F. ) ;
#27097=CARTESIAN_POINT ( 'NONE',  ( -6.489213562373093325, -27.52281430457059841, 5.000000000000000000 ) ) ;
#27098=EDGE_LOOP ( 'NONE', ( #78878, #19768, #78182, #32617 ) ) ;
#27100=VERTEX_POINT ( 'NONE', #40796 ) ;
#27101=ORIENTED_EDGE ( 'NONE', *, *, #130577, .T. ) ;
#27102=LINE ( 'NONE', #138740, #140357 ) ;
#27103=CARTESIAN_POINT ( 'NONE',  ( 27.18398860626900060, 28.73617430169806042, 5.000000000000000000 ) ) ;
#27104=CARTESIAN_POINT ( 'NONE',  ( -17.99999999999986855, -16.02097659208072145, -11.96015758381204286 ) ) ;
#27105=DIRECTION ( 'NONE',  ( 0.7071067811865487940, 0.7071067811865463515, 0.000000000000000000 ) ) ;
#27108=ORIENTED_EDGE ( 'NONE', *, *, #140260, .F. ) ;
#27109=CARTESIAN_POINT ( 'NONE',  ( -27.70898713287128956, 22.22500000000000142, 7.734417024081176706 ) ) ;
#27110=DIRECTION ( 'NONE',  ( 0.7071067811865486830, -0.7071067811865464625, -0.000000000000000000 ) ) ;
#27112=VECTOR ( 'NONE', #3310, 1000.000000000000000 ) ;
#27113=CARTESIAN_POINT ( 'NONE',  ( -34.49999999999976552, -14.94567065516890558, 4.994342998332162331 ) ) ;
#27114=DIRECTION ( 'NONE',  ( 0.3543493200069162685, -0.000000000000000000, -0.9351131265310288487 ) ) ;
#27118=VECTOR ( 'NONE', #48208, 1000.000000000000000 ) ;
#27120=VERTEX_POINT ( 'NONE', #85696 ) ;
#27121=VERTEX_POINT ( 'NONE', #73429 ) ;
#27123=FACE_OUTER_BOUND ( 'NONE', #117085, .T. ) ;
#27124=EDGE_CURVE ( 'NONE', #63599, #22463, #32050, .T. ) ;
#27125=FACE_OUTER_BOUND ( 'NONE', #78405, .T. ) ;
#27126=DIRECTION ( 'NONE',  ( -0.7071067811865486830, -0.7071067811865464625, -0.000000000000000000 ) ) ;
#27127=EDGE_CURVE ( 'NONE', #32567, #36781, #108860, .T. ) ;
#27128=VECTOR ( 'NONE', #77912, 1000.000000000000000 ) ;
#27130=EDGE_CURVE ( 'NONE', #98666, #40296, #106731, .T. ) ;
#27132=DIRECTION ( 'NONE',  ( 0.7071067811865487940, 0.7071067811865463515, -0.000000000000000000 ) ) ;
#27135=VECTOR ( 'NONE', #7850, 1000.000000000000000 ) ;
#27136=CARTESIAN_POINT ( 'NONE',  ( -26.99451991528749417, 28.92564299267956685, 4.000000000000000000 ) ) ;
#27137=VERTEX_POINT ( 'NONE', #131367 ) ;
#27138=VERTEX_POINT ( 'NONE', #76284 ) ;
#27139=DIRECTION ( 'NONE',  ( -0.6830127018922181881, 0.6830127018922202975, -0.2588190451025214056 ) ) ;
#27140=DIRECTION ( 'NONE',  ( 0.6830127018922180770, -0.6830127018922204085, -0.2588190451025213501 ) ) ;
#27141=FACE_OUTER_BOUND ( 'NONE', #104491, .T. ) ;
#27142=EDGE_CURVE ( 'NONE', #20400, #47125, #19735, .T. ) ;
#27143=DIRECTION ( 'NONE',  ( -0.6830127018922180770, -0.6830127018922204085, -0.2588190451025213501 ) ) ;
#27144=EDGE_CURVE ( 'NONE', #35648, #63600, #95869, .T. ) ;
#27145=DIRECTION ( 'NONE',  ( 0.7071067811865487940, -0.7071067811865463515, 0.000000000000000000 ) ) ;
#27147=ORIENTED_EDGE ( 'NONE', *, *, #137345, .F. ) ;
#27148=LINE ( 'NONE', #106108, #110896 ) ;
#27149=FACE_OUTER_BOUND ( 'NONE', #36811, .T. ) ;
#27150=DIRECTION ( 'NONE',  ( -0.7071067811865486830, -0.7071067811865464625, 0.000000000000000000 ) ) ;
#27151=CARTESIAN_POINT ( 'NONE',  ( 44.99451991528749772, 28.92564299267969474, 4.000000000000000000 ) ) ;
#27152=EDGE_CURVE ( 'NONE', #39448, #72881, #120438, .T. ) ;
#27153=VERTEX_POINT ( 'NONE', #129204 ) ;
#27154=ORIENTED_EDGE ( 'NONE', *, *, #17351, .F. ) ;
#27157=PLANE ( 'NONE',  #126521 ) ;
#27159=EDGE_LOOP ( 'NONE', ( #57738, #126429, #112627, #95023 ) ) ;
#27161=EDGE_CURVE ( 'NONE', #25602, #49545, #96551, .T. ) ;
#27163=CARTESIAN_POINT ( 'NONE',  ( -1.228506771386643770, 20.25929247661551003, 7.808871592221766633 ) ) ;
#27164=VERTEX_POINT ( 'NONE', #9554 ) ;
#27165=ORIENTED_EDGE ( 'NONE', *, *, #129738, .F. ) ;
#27166=CARTESIAN_POINT ( 'NONE',  ( -17.20710678118642178, -8.240707523384195099, 5.000000000000000000 ) ) ;
#27167=ORIENTED_EDGE ( 'NONE', *, *, #47160, .T. ) ;
#27168=CARTESIAN_POINT ( 'NONE',  ( 0.000000000000000000, 0.000000000000000000, 5.000000000000000000 ) ) ;
#27169=EDGE_CURVE ( 'NONE', #126557, #15065, #95155, .T. ) ;
#27170=FACE_OUTER_BOUND ( 'NONE', #4690, .T. ) ;
#27172=FACE_BOUND ( 'NONE', #61531, .T. ) ;
#27173=CARTESIAN_POINT ( 'NONE',  ( 63.48921356237309510, -27.52281430457099631, 5.000000000000000000 ) ) ;
#27174=CARTESIAN_POINT ( 'NONE',  ( -21.18398860626899349, 28.73617430169802134, 5.000000000000000000 ) ) ;
#27176=LINE ( 'NONE', #84452, #103727 ) ;
#27179=EDGE_CURVE ( 'NONE', #31209, #15110, #8807, .T. ) ;
#27182=ORIENTED_EDGE ( 'NONE', *, *, #122526, .T. ) ;
#27185=DIRECTION ( 'NONE',  ( 0.7071067811865487940, -0.7071067811865463515, 0.000000000000000000 ) ) ;
#27186=VECTOR ( 'NONE', #110743, 1000.000000000000000 ) ;
#27187=LINE ( 'NONE', #72181, #81469 ) ;
#27188=CARTESIAN_POINT ( 'NONE',  ( -4.499999999999967137, 16.77039438581778796, 0.4657186855307844375 ) ) ;
#27190=ORIENTED_EDGE ( 'NONE', *, *, #24251, .T. ) ;
#27191=LINE ( 'NONE', #83763, #15945 ) ;
#27193=EDGE_CURVE ( 'NONE', #103105, #129709, #97263, .T. ) ;
#27194=CARTESIAN_POINT ( 'NONE',  ( -2.816011393730999401, 28.73617430169785436, 5.000000000000000000 ) ) ;
#27195=LINE ( 'NONE', #108842, #62115 ) ;
#27196=DIRECTION ( 'NONE',  ( -0.000000000000000000, 0.3543493200069153248, 0.9351131265310292928 ) ) ;
#27197=DIRECTION ( 'NONE',  ( -0.7071067811865486830, 0.7071067811865464625, 0.000000000000000000 ) ) ;
#27199=CARTESIAN_POINT ( 'NONE',  ( 20.99999999999983658, -22.22500000000000142, 4.412002311789984255 ) ) ;
#27200=ORIENTED_EDGE ( 'NONE', *, *, #140070, .F. ) ;
#27201=LINE ( 'NONE', #93891, #56616 ) ;
#27202=CARTESIAN_POINT ( 'NONE',  ( -4.171830600776442743, -14.24070752338413648, 4.000000000000000000 ) ) ;
#27203=ORIENTED_EDGE ( 'NONE', *, *, #136295, .T. ) ;
#27204=ORIENTED_EDGE ( 'NONE', *, *, #48479, .T. ) ;
#27205=EDGE_CURVE ( 'NONE', #90987, #66739, #111009, .T. ) ;
#27206=VERTEX_POINT ( 'NONE', #123368 ) ;
#27208=AXIS2_PLACEMENT_3D ( 'NONE', #81475, #103185, #37223 ) ;
#27213=VERTEX_POINT ( 'NONE', #111758 ) ;
#27214=CARTESIAN_POINT ( 'NONE',  ( -51.29974487139158867, -27.71228299555242103, 4.000000000000000000 ) ) ;
#27215=VERTEX_POINT ( 'NONE', #12425 ) ;
#27217=CARTESIAN_POINT ( 'NONE',  ( -10.49999999999992184, -7.533600742197662292, 5.000000000000000000 ) ) ;
#27218=CARTESIAN_POINT ( 'NONE',  ( -34.92500000000001137, -22.22500000000000142, 5.000000000000000000 ) ) ;
#27219=ORIENTED_EDGE ( 'NONE', *, *, #124288, .F. ) ;
#27220=ORIENTED_EDGE ( 'NONE', *, *, #86410, .T. ) ;
#27221=CARTESIAN_POINT ( 'NONE',  ( -34.49999999999975842, -11.94567065516892690, 4.994342998332167660 ) ) ;
#27223=VERTEX_POINT ( 'NONE', #56705 ) ;
#27224=PLANE ( 'NONE',  #82871 ) ;
#27225=ORIENTED_EDGE ( 'NONE', *, *, #103716, .F. ) ;
#27227=ORIENTED_EDGE ( 'NONE', *, *, #83239, .T. ) ;
#27228=ORIENTED_EDGE ( 'NONE', *, *, #101625, .F. ) ;
#27231=CARTESIAN_POINT ( 'NONE',  ( -17.57672154193636160, 11.25929247661559529, 17.85071094206588427 ) ) ;
#27232=DIRECTION ( 'NONE',  ( -0.7071067811865486830, -0.7071067811865464625, 0.000000000000000000 ) ) ;
#27233=ADVANCED_FACE ( 'NONE', ( #101570 ), #68292, .F. ) ;
#27234=LINE ( 'NONE', #127266, #122417 ) ;
#27235=ADVANCED_FACE ( 'NONE', ( #21878 ), #21170, .F. ) ;
#27236=LINE ( 'NONE', #71481, #97589 ) ;
#27237=ORIENTED_EDGE ( 'NONE', *, *, #102774, .T. ) ;
#27238=CARTESIAN_POINT ( 'NONE',  ( 27.18398860626900060, 28.73617430169806042, 5.000000000000000000 ) ) ;
#27240=PLANE ( 'NONE',  #71680 ) ;
#27241=CARTESIAN_POINT ( 'NONE',  ( -15.18398860626900237, 28.73617430169797871, 5.000000000000000000 ) ) ;
#27243=EDGE_CURVE ( 'NONE', #27246, #104944, #43635, .T. ) ;
#27244=FACE_OUTER_BOUND ( 'NONE', #129947, .T. ) ;
#27246=VERTEX_POINT ( 'NONE', #134964 ) ;
#27247=ORIENTED_EDGE ( 'NONE', *, *, #66929, .T. ) ;
#27248=CARTESIAN_POINT ( 'NONE',  ( 5.816011393731002066, 28.73617430169783304, 5.000000000000000000 ) ) ;
#27249=DIRECTION ( 'NONE',  ( 0.6830127018922181881, 0.6830127018922202975, -0.2588190451025214056 ) ) ;
#27251=CARTESIAN_POINT ( 'NONE',  ( -11.99451991528749417, 28.92564299267946382, 4.000000000000000000 ) ) ;
#27252=CARTESIAN_POINT ( 'NONE',  ( 34.49999999999976552, 1.087461875839230707, 4.000000000000000000 ) ) ;
#27253=CARTESIAN_POINT ( 'NONE',  ( 24.60486233187506855, 21.75929247661550647, 21.32995629748181088 ) ) ;
#27255=EDGE_CURVE ( 'NONE', #16368, #122297, #133512, .T. ) ;
#27257=DIRECTION ( 'NONE',  ( -0.7071067811865486830, -0.7071067811865464625, 0.000000000000000000 ) ) ;
#27258=VECTOR ( 'NONE', #19805, 1000.000000000000000 ) ;
#27260=DIRECTION ( 'NONE',  ( -0.000000000000000000, -0.3543493200069152693, 0.9351131265310292928 ) ) ;
#27261=DIRECTION ( 'NONE',  ( 0.6830127018922180770, -0.6830127018922204085, -0.2588190451025213501 ) ) ;
#27262=ORIENTED_EDGE ( 'NONE', *, *, #17321, .F. ) ;
#27264=ORIENTED_EDGE ( 'NONE', *, *, #86785, .T. ) ;
#27265=VECTOR ( 'NONE', #93206, 1000.000000000000000 ) ;
#27266=CARTESIAN_POINT ( 'NONE',  ( -30.48921356237309510, -27.52281430457076894, 5.000000000000000000 ) ) ;
#27268=VERTEX_POINT ( 'NONE', #121886 ) ;
#27269=VECTOR ( 'NONE', #3112, 1000.000000000000000 ) ;
#27270=CARTESIAN_POINT ( 'NONE',  ( -42.48921356237308800, -27.52281430457085065, 5.000000000000000000 ) ) ;
#27271=LINE ( 'NONE', #93257, #109692 ) ;
#27273=CARTESIAN_POINT ( 'NONE',  ( -28.49999999999979750, -13.91253812416061386, 4.000000000000000000 ) ) ;
#27274=ORIENTED_EDGE ( 'NONE', *, *, #80634, .F. ) ;
#27275=CARTESIAN_POINT ( 'NONE',  ( -8.700255128608413102, -27.71228299555199825, 4.000000000000000000 ) ) ;
#27277=CARTESIAN_POINT ( 'NONE',  ( 69.18398860626899705, 28.73617430169835529, 5.000000000000000000 ) ) ;
#27280=ADVANCED_FACE ( 'NONE', ( #44389 ), #22560, .F. ) ;
#27282=ORIENTED_EDGE ( 'NONE', *, *, #88553, .F. ) ;
#27284=EDGE_CURVE ( 'NONE', #90422, #47233, #66128, .T. ) ;
#27285=CARTESIAN_POINT ( 'NONE',  ( 42.48921356237308800, -27.52281430457085065, 5.000000000000000000 ) ) ;
#27287=CARTESIAN_POINT ( 'NONE',  ( -7.499999999999940492, 10.46639925780215208, 5.000000000000000000 ) ) ;
#27288=CARTESIAN_POINT ( 'NONE',  ( 5.999999999999960032, -19.06887692260762179, 4.000000000000000000 ) ) ;
#27289=VERTEX_POINT ( 'NONE', #2235 ) ;
#27290=EDGE_CURVE ( 'NONE', #37516, #141779, #11685, .T. ) ;
#27293=ORIENTED_EDGE ( 'NONE', *, *, #47177, .F. ) ;
#27295=CARTESIAN_POINT ( 'NONE',  ( 32.99451991528749062, 28.92564299267960948, 4.000000000000000000 ) ) ;
#27296=LINE ( 'NONE', #28760, #97840 ) ;
#27297=DIRECTION ( 'NONE',  ( 0.6830127018922180770, -0.6830127018922204085, -0.2588190451025213501 ) ) ;
#27298=VERTEX_POINT ( 'NONE', #88594 ) ;
#27299=LINE ( 'NONE', #96126, #139216 ) ;
#27300=LINE ( 'NONE', #26608, #136756 ) ;
#27301=EDGE_CURVE ( 'NONE', #22851, #107195, #10279, .T. ) ;
#27303=EDGE_CURVE ( 'NONE', #105156, #113756, #34922, .T. ) ;
#27305=DIRECTION ( 'NONE',  ( -0.000000000000000000, 0.000000000000000000, 1.000000000000000000 ) ) ;
#27308=VECTOR ( 'NONE', #98006, 999.9999999999998863 ) ;
#27309=CARTESIAN_POINT ( 'NONE',  ( -19.88982677111775388, -22.22500000000000142, 4.785647885939353863 ) ) ;
#27312=ORIENTED_EDGE ( 'NONE', *, *, #16847, .F. ) ;
#27313=VERTEX_POINT ( 'NONE', #33509 ) ;
#27314=VERTEX_POINT ( 'NONE', #66827 ) ;
#27316=ORIENTED_EDGE ( 'NONE', *, *, #8960, .F. ) ;
#27317=ADVANCED_FACE ( 'NONE', ( #100175 ), #822, .F. ) ;
#27318=PLANE ( 'NONE',  #5725 ) ;
#27323=ADVANCED_FACE ( 'NONE', ( #35658 ), #67566, .F. ) ;
#27324=DIRECTION ( 'NONE',  ( 0.7071067811865486830, -0.7071067811865464625, -0.000000000000000000 ) ) ;
#27325=DIRECTION ( 'NONE',  ( -0.000000000000000000, 0.3543493200069153248, 0.9351131265310291818 ) ) ;
#27326=VECTOR ( 'NONE', #69943, 1000.000000000000227 ) ;
#27329=FACE_OUTER_BOUND ( 'NONE', #87629, .T. ) ;
#27332=EDGE_LOOP ( 'NONE', ( #19956, #77522, #135414, #20382 ) ) ;
#27333=EDGE_LOOP ( 'NONE', ( #50597, #7173, #93192, #104103 ) ) ;
#27334=CARTESIAN_POINT ( 'NONE',  ( 24.27626632409106477, -22.22500000000000142, 27.43357286974619669 ) ) ;
#27335=FACE_OUTER_BOUND ( 'NONE', #107760, .T. ) ;
#27337=LINE ( 'NONE', #73716, #72004 ) ;
#27338=CARTESIAN_POINT ( 'NONE',  ( 11.99999999999991296, -13.97847968911259109, -0.1324546996126522713 ) ) ;
#27341=LINE ( 'NONE', #73044, #60470 ) ;
#27342=ADVANCED_FACE ( 'NONE', ( #125491 ), #37776, .F. ) ;
#27343=ORIENTED_EDGE ( 'NONE', *, *, #119876, .F. ) ;
#27344=ORIENTED_EDGE ( 'NONE', *, *, #96496, .T. ) ;
#27345=VECTOR ( 'NONE', #10433, 1000.000000000000000 ) ;
#27346=ORIENTED_EDGE ( 'NONE', *, *, #27144, .T. ) ;
#27348=FACE_OUTER_BOUND ( 'NONE', #104031, .T. ) ;
#27349=ORIENTED_EDGE ( 'NONE', *, *, #94836, .T. ) ;
#27350=CARTESIAN_POINT ( 'NONE',  ( -20.99999999999986500, 14.87792677143806941, -11.06722581663444771 ) ) ;
#27351=DIRECTION ( 'NONE',  ( -0.7071067811865486830, -0.7071067811865464625, 0.000000000000000000 ) ) ;
#27352=CARTESIAN_POINT ( 'NONE',  ( -50.99451991528749062, 28.92564299267973738, 4.000000000000000000 ) ) ;
#27353=DIRECTION ( 'NONE',  ( 0.7071067811865487940, -0.7071067811865463515, 0.000000000000000000 ) ) ;
#27354=VECTOR ( 'NONE', #105673, 1000.000000000000000 ) ;
#27355=DIRECTION ( 'NONE',  ( 0.7071067811865487940, 0.7071067811865463515, -0.000000000000000000 ) ) ;
#27356=ORIENTED_EDGE ( 'NONE', *, *, #91186, .F. ) ;
#27358=DIRECTION ( 'NONE',  ( -0.6830127018922180770, -0.6830127018922204085, -0.2588190451025213501 ) ) ;
#27359=ORIENTED_EDGE ( 'NONE', *, *, #102990, .F. ) ;
#27360=CARTESIAN_POINT ( 'NONE',  ( -28.17183060077627843, -2.240707523384257716, 4.000000000000000000 ) ) ;
#27361=ORIENTED_EDGE ( 'NONE', *, *, #14169, .F. ) ;
#27362=VERTEX_POINT ( 'NONE', #92119 ) ;
#27363=PLANE ( 'NONE',  #1878 ) ;
#27364=ORIENTED_EDGE ( 'NONE', *, *, #127528, .T. ) ;
#27365=ORIENTED_EDGE ( 'NONE', *, *, #131799, .T. ) ;
#27367=VECTOR ( 'NONE', #100327, 1000.000000000000000 ) ;
#27369=VECTOR ( 'NONE', #29682, 1000.000000000000000 ) ;
#27371=DIRECTION ( 'NONE',  ( -0.3543493200069162685, -0.000000000000000000, -0.9351131265310288487 ) ) ;
#27375=CARTESIAN_POINT ( 'NONE',  ( 30.18398860626900060, 28.73617430169808173, 5.000000000000000000 ) ) ;
#27377=DIRECTION ( 'NONE',  ( -0.6830127018922181881, 0.6830127018922202975, -0.2588190451025214056 ) ) ;
#27380=DIRECTION ( 'NONE',  ( -0.000000000000000000, 0.000000000000000000, 1.000000000000000000 ) ) ;
#27381=CARTESIAN_POINT ( 'NONE',  ( -11.99451991528749417, 28.92564299267946382, 4.000000000000000000 ) ) ;
#27382=CARTESIAN_POINT ( 'NONE',  ( -1.499999999999990896, 21.43112307739196609, 4.000000000000000000 ) ) ;
#27383=ORIENTED_EDGE ( 'NONE', *, *, #31327, .T. ) ;
#27385=CARTESIAN_POINT ( 'NONE',  ( -48.18398860626899705, 28.73617430169820608, 5.000000000000000000 ) ) ;
#27388=VECTOR ( 'NONE', #67076, 999.9999999999998863 ) ;
#27389=LINE ( 'NONE', #15768, #135176 ) ;
#27390=ORIENTED_EDGE ( 'NONE', *, *, #28430, .T. ) ;
#27391=VECTOR ( 'NONE', #93066, 1000.000000000000000 ) ;
#27392=DIRECTION ( 'NONE',  ( -0.7071067811865486830, 0.7071067811865464625, 0.000000000000000000 ) ) ;
#27394=VECTOR ( 'NONE', #62365, 999.9999999999998863 ) ;
#27396=PLANE ( 'NONE',  #69511 ) ;
#27397=DIRECTION ( 'NONE',  ( 0.6830127018922181881, 0.6830127018922202975, -0.2588190451025214056 ) ) ;
#27398=ORIENTED_EDGE ( 'NONE', *, *, #34695, .F. ) ;
#27399=ADVANCED_FACE ( 'NONE', ( #80569 ), #39193, .F. ) ;
#27401=ORIENTED_EDGE ( 'NONE', *, *, #131043, .F. ) ;
#27406=EDGE_CURVE ( 'NONE', #75064, #90194, #91437, .T. ) ;
#27407=DIRECTION ( 'NONE',  ( 0.7071067811865487940, 0.7071067811865463515, 0.000000000000000000 ) ) ;
#27411=EDGE_LOOP ( 'NONE', ( #17700, #115430, #7606, #88964 ) ) ;
#27412=LINE ( 'NONE', #126054, #919 ) ;
#27413=CARTESIAN_POINT ( 'NONE',  ( 33.70710678118631165, 20.25929247661551003, 5.000000000000000000 ) ) ;
#27414=FACE_OUTER_BOUND ( 'NONE', #70257, .T. ) ;
#27415=VECTOR ( 'NONE', #63087, 1000.000000000000000 ) ;
#27416=CARTESIAN_POINT ( 'NONE',  ( -19.82816939922339827, -14.24070752338414181, 4.000000000000000000 ) ) ;
#27417=CARTESIAN_POINT ( 'NONE',  ( 21.29974487139158512, -27.71228299555221142, 4.000000000000000000 ) ) ;
#27418=CARTESIAN_POINT ( 'NONE',  ( -30.48921356237309510, -27.52281430457076894, 5.000000000000000000 ) ) ;
#27419=ADVANCED_FACE ( 'NONE', ( #103018 ), #25436, .F. ) ;
#27420=CARTESIAN_POINT ( 'NONE',  ( 45.48921356237309510, -27.52281430457087197, 5.000000000000000000 ) ) ;
#27421=CARTESIAN_POINT ( 'NONE',  ( -24.29974487139158867, -27.71228299555223273, 4.000000000000000000 ) ) ;
#27422=DIRECTION ( 'NONE',  ( 0.6830127018922180770, -0.6830127018922204085, -0.2588190451025213501 ) ) ;
#27423=ORIENTED_EDGE ( 'NONE', *, *, #48068, .T. ) ;
#27425=EDGE_CURVE ( 'NONE', #39039, #6977, #124057, .T. ) ;
#27426=CARTESIAN_POINT ( 'NONE',  ( 32.99451991528749062, 28.92564299267960948, 4.000000000000000000 ) ) ;
#27427=ORIENTED_EDGE ( 'NONE', *, *, #72986, .F. ) ;
#27428=DIRECTION ( 'NONE',  ( 0.7071067811865487940, 0.7071067811865463515, 0.000000000000000000 ) ) ;
#27429=FACE_OUTER_BOUND ( 'NONE', #52218, .T. ) ;
#27430=ORIENTED_EDGE ( 'NONE', *, *, #80883, .T. ) ;
#27433=FACE_OUTER_BOUND ( 'NONE', #45050, .T. ) ;
#27434=CARTESIAN_POINT ( 'NONE',  ( 11.99999999999991473, -19.22509904557635707, 1.855685503482207510 ) ) ;
#27435=EDGE_CURVE ( 'NONE', #55364, #132228, #47954, .T. ) ;
#27436=ORIENTED_EDGE ( 'NONE', *, *, #74856, .T. ) ;
#27437=VERTEX_POINT ( 'NONE', #69703 ) ;
#27438=LINE ( 'NONE', #105011, #82262 ) ;
#27439=DIRECTION ( 'NONE',  ( -0.000000000000000000, 0.000000000000000000, 1.000000000000000000 ) ) ;
#27441=FACE_OUTER_BOUND ( 'NONE', #109799, .T. ) ;
#27442=CARTESIAN_POINT ( 'NONE',  ( 34.92499999999998295, 17.71849043720409256, 4.759050581649320932 ) ) ;
#27444=FACE_OUTER_BOUND ( 'NONE', #97075, .T. ) ;
#27445=EDGE_CURVE ( 'NONE', #139988, #128738, #126881, .T. ) ;
#27449=LINE ( 'NONE', #5693, #39007 ) ;
#27450=PLANE ( 'NONE',  #139310 ) ;
#27451=LINE ( 'NONE', #84036, #26998 ) ;
#27452=ORIENTED_EDGE ( 'NONE', *, *, #49428, .T. ) ;
#27454=ORIENTED_EDGE ( 'NONE', *, *, #121698, .T. ) ;
#27458=ORIENTED_EDGE ( 'NONE', *, *, #108285, .T. ) ;
#27459=ORIENTED_EDGE ( 'NONE', *, *, #24251, .F. ) ;
#27460=FACE_OUTER_BOUND ( 'NONE', #28180, .T. ) ;
#27461=CARTESIAN_POINT ( 'NONE',  ( -1.956830458227830416, -22.22500000000000142, 17.49287185427191460 ) ) ;
#27462=ORIENTED_EDGE ( 'NONE', *, *, #107627, .F. ) ;
#27463=VECTOR ( 'NONE', #7740, 1000.000000000000000 ) ;
#27464=VECTOR ( 'NONE', #53468, 1000.000000000000000 ) ;
#27465=VECTOR ( 'NONE', #47223, 1000.000000000000000 ) ;
#27466=DIRECTION ( 'NONE',  ( -0.6830127018922181881, 0.6830127018922202975, -0.2588190451025214056 ) ) ;
#27468=FACE_OUTER_BOUND ( 'NONE', #126771, .T. ) ;
#27469=VECTOR ( 'NONE', #104378, 1000.000000000000000 ) ;
#27470=CARTESIAN_POINT ( 'NONE',  ( 29.47599861414531475, 22.03583458319438293, 4.979811245910086726 ) ) ;
#27472=EDGE_CURVE ( 'NONE', #99005, #110390, #94268, .T. ) ;
#27473=CARTESIAN_POINT ( 'NONE',  ( 32.99999999999977263, -16.06887692260765377, 4.000000000000000000 ) ) ;
#27474=FACE_OUTER_BOUND ( 'NONE', #96547, .T. ) ;
#27476=VECTOR ( 'NONE', #98011, 1000.000000000000227 ) ;
#27477=PLANE ( 'NONE',  #75336 ) ;
#27478=PLANE ( 'NONE',  #30780 ) ;
#27479=CARTESIAN_POINT ( 'NONE',  ( 34.82816939922328459, -8.240707523384196875, 4.000000000000000000 ) ) ;
#27480=AXIS2_PLACEMENT_3D ( 'NONE', #23519, #47473, #15463 ) ;
#27481=CARTESIAN_POINT ( 'NONE',  ( -39.48921356237310221, -27.52281430457082934, 5.000000000000000000 ) ) ;
#27482=ORIENTED_EDGE ( 'NONE', *, *, #594, .T. ) ;
#27483=ORIENTED_EDGE ( 'NONE', *, *, #10619, .F. ) ;
#27485=ORIENTED_EDGE ( 'NONE', *, *, #139619, .T. ) ;
#27486=ADVANCED_FACE ( 'NONE', ( #116008 ), #24732, .T. ) ;
#27487=FACE_OUTER_BOUND ( 'NONE', #121615, .T. ) ;
#27490=LINE ( 'NONE', #28946, #42152 ) ;
#27491=LINE ( 'NONE', #107207, #139270 ) ;
#27492=VECTOR ( 'NONE', #106991, 1000.000000000000000 ) ;
#27494=ORIENTED_EDGE ( 'NONE', *, *, #22708, .F. ) ;
#27495=CARTESIAN_POINT ( 'NONE',  ( -2.241399257802041856, 21.72499999999999432, 5.000000000000000000 ) ) ;
#27496=ORIENTED_EDGE ( 'NONE', *, *, #92334, .F. ) ;
#27497=PLANE ( 'NONE',  #77785 ) ;
#27498=VECTOR ( 'NONE', #63166, 999.9999999999998863 ) ;
#27499=CARTESIAN_POINT ( 'NONE',  ( 34.92499999999998295, 13.51246187583934955, 4.000000000000000000 ) ) ;
#27500=CARTESIAN_POINT ( 'NONE',  ( 32.58838509405146056, 22.22500000000000497, 4.777194822843813249 ) ) ;
#27501=VECTOR ( 'NONE', #128439, 999.9999999999998863 ) ;
#27502=VECTOR ( 'NONE', #3361, 1000.000000000000000 ) ;
#27504=VERTEX_POINT ( 'NONE', #72583 ) ;
#27505=ORIENTED_EDGE ( 'NONE', *, *, #54200, .F. ) ;
#27506=ORIENTED_EDGE ( 'NONE', *, *, #12062, .T. ) ;
#27508=LINE ( 'NONE', #10049, #89368 ) ;
#27510=AXIS2_PLACEMENT_3D ( 'NONE', #123243, #47841, #36909 ) ;
#27511=VECTOR ( 'NONE', #21691, 1000.000000000000000 ) ;
#27512=LINE ( 'NONE', #13243, #24797 ) ;
#27513=EDGE_CURVE ( 'NONE', #13138, #42047, #116741, .T. ) ;
#27516=ORIENTED_EDGE ( 'NONE', *, *, #35678, .F. ) ;
#27517=ORIENTED_EDGE ( 'NONE', *, *, #14709, .T. ) ;
#27518=DIRECTION ( 'NONE',  ( -0.3543493200069163240, 4.681814790819596721E-17, -0.9351131265310288487 ) ) ;
#27519=ORIENTED_EDGE ( 'NONE', *, *, #64484, .T. ) ;
#27520=EDGE_LOOP ( 'NONE', ( #103009, #8488, #74126, #6497 ) ) ;
#27521=VECTOR ( 'NONE', #72061, 1000.000000000000227 ) ;
#27523=LINE ( 'NONE', #3611, #97545 ) ;
#27524=CARTESIAN_POINT ( 'NONE',  ( -3.851816449618530758, 17.25929247661554911, 8.802941693769193776 ) ) ;
#27525=ORIENTED_EDGE ( 'NONE', *, *, #103521, .F. ) ;
#27526=DIRECTION ( 'NONE',  ( -0.6830127018922181881, 0.6830127018922202975, -0.2588190451025214056 ) ) ;
#27527=DIRECTION ( 'NONE',  ( 0.6830127018922180770, -0.6830127018922204085, -0.2588190451025213501 ) ) ;
#27528=PLANE ( 'NONE',  #127021 ) ;
#27530=ORIENTED_EDGE ( 'NONE', *, *, #66589, .T. ) ;
#27531=CARTESIAN_POINT ( 'NONE',  ( -19.61351471301484750, 9.118430946277902294, 4.525620927308363406 ) ) ;
#27532=FACE_BOUND ( 'NONE', #55297, .T. ) ;
#27533=ORIENTED_EDGE ( 'NONE', *, *, #130847, .T. ) ;
#27535=LINE ( 'NONE', #61642, #15654 ) ;
#27536=FACE_OUTER_BOUND ( 'NONE', #32334, .T. ) ;
#27537=EDGE_LOOP ( 'NONE', ( #733, #22451, #10611, #40769 ) ) ;
#27538=FACE_OUTER_BOUND ( 'NONE', #79746, .T. ) ;
#27539=ORIENTED_EDGE ( 'NONE', *, *, #23256, .F. ) ;
#27540=ORIENTED_EDGE ( 'NONE', *, *, #63621, .T. ) ;
#27541=ORIENTED_EDGE ( 'NONE', *, *, #13327, .F. ) ;
#27543=ORIENTED_EDGE ( 'NONE', *, *, #24429, .T. ) ;
#27544=CARTESIAN_POINT ( 'NONE',  ( 19.05000000000000071, 3.174999999999997158, 4.000000000000000000 ) ) ;
#27547=ADVANCED_FACE ( 'NONE', ( #6498 ), #94968, .F. ) ;
#27549=DIRECTION ( 'NONE',  ( 0.7071067811865487940, -0.7071067811865463515, 0.000000000000000000 ) ) ;
#27550=CARTESIAN_POINT ( 'NONE',  ( -18.33010218547253345, 17.25929247661553845, 19.83885114516075632 ) ) ;
#27553=CARTESIAN_POINT ( 'NONE',  ( 18.48921356237309510, -27.52281430457068367, 5.000000000000000000 ) ) ;
#27554=DIRECTION ( 'NONE',  ( -0.7071067811865486830, -0.7071067811865464625, 0.000000000000000000 ) ) ;
#27555=PLANE ( 'NONE',  #109530 ) ;
#27557=VERTEX_POINT ( 'NONE', #74696 ) ;
#27559=VERTEX_POINT ( 'NONE', #73959 ) ;
#27560=ORIENTED_EDGE ( 'NONE', *, *, #43514, .F. ) ;
#27561=LINE ( 'NONE', #71831, #54157 ) ;
#27562=VECTOR ( 'NONE', #92094, 1000.000000000000227 ) ;
#27564=EDGE_LOOP ( 'NONE', ( #106558, #124021, #5866, #16526 ) ) ;
#27565=VECTOR ( 'NONE', #14846, 1000.000000000000000 ) ;
#27566=( BOUNDED_CURVE ( )  B_SPLINE_CURVE ( 3, ( #115039, #15034, #70887, #82462 ),
 .UNSPECIFIED., .F., .T. ) 
 B_SPLINE_CURVE_WITH_KNOTS ( ( 4, 4 ),
 ( 1.901594255663603183, 1.933014472006554740 ),
 .UNSPECIFIED. ) 
 CURVE ( )  GEOMETRIC_REPRESENTATION_ITEM ( )  RATIONAL_B_SPLINE_CURVE ( ( 1.000000000000000000, 0.9999177325257868620, 0.9999177325257868620, 1.000000000000000000 ) ) 
 REPRESENTATION_ITEM ( '' )  );
#27567=EDGE_CURVE ( 'NONE', #28113, #133506, #20264, .T. ) ;
#27568=EDGE_LOOP ( 'NONE', ( #76928, #116368, #4757, #67538 ) ) ;
#27569=FACE_OUTER_BOUND ( 'NONE', #119856, .T. ) ;
#27570=DIRECTION ( 'NONE',  ( -0.7071067811865486830, 0.7071067811865464625, 0.000000000000000000 ) ) ;
#27571=EDGE_CURVE ( 'NONE', #110890, #139365, #128353, .T. ) ;
#27572=EDGE_CURVE ( 'NONE', #47491, #141426, #18843, .T. ) ;
#27573=CARTESIAN_POINT ( 'NONE',  ( 6.183988606268994381, 28.73617430169791476, 5.000000000000000000 ) ) ;
#27574=ORIENTED_EDGE ( 'NONE', *, *, #113028, .T. ) ;
#27577=VERTEX_POINT ( 'NONE', #31179 ) ;
#27578=CARTESIAN_POINT ( 'NONE',  ( -24.32816939922335919, 8.259292476615634371, 4.000000000000000000 ) ) ;
#27579=EDGE_CURVE ( 'NONE', #83894, #92198, #32373, .T. ) ;
#27580=ADVANCED_FACE ( 'NONE', ( #29024 ), #39934, .F. ) ;
#27583=VERTEX_POINT ( 'NONE', #52195 ) ;
#27585=CARTESIAN_POINT ( 'NONE',  ( -38.57672154193621594, 11.25929247661560240, 17.85071094206593401 ) ) ;
#27586=ADVANCED_FACE ( 'NONE', ( #51506 ), #118877, .F. ) ;
#27587=CARTESIAN_POINT ( 'NONE',  ( 16.00193056682086379, -22.22500000000000142, 4.500000000000000888 ) ) ;
#27588=ORIENTED_EDGE ( 'NONE', *, *, #1887, .F. ) ;
#27589=ORIENTED_EDGE ( 'NONE', *, *, #131094, .F. ) ;
#27590=FACE_OUTER_BOUND ( 'NONE', #57545, .T. ) ;
#27591=ORIENTED_EDGE ( 'NONE', *, *, #32114, .F. ) ;
#27594=LINE ( 'NONE', #15267, #101961 ) ;
#27596=CARTESIAN_POINT ( 'NONE',  ( -36.18398860626899705, 28.73617430169812437, 5.000000000000000000 ) ) ;
#27597=CARTESIAN_POINT ( 'NONE',  ( 34.92499999999998295, -14.33753812416083129, 4.000000000000000000 ) ) ;
#27599=VERTEX_POINT ( 'NONE', #7957 ) ;
#27600=DIRECTION ( 'NONE',  ( 0.7071067811865487940, -0.7071067811865463515, 0.000000000000000000 ) ) ;
#27601=EDGE_CURVE ( 'NONE', #118949, #5220, #108680, .T. ) ;
#27604=PLANE ( 'NONE',  #104737 ) ;
#27605=VERTEX_POINT ( 'NONE', #95697 ) ;
#27606=CARTESIAN_POINT ( 'NONE',  ( 15.48921356237309510, -27.52281430457066236, 5.000000000000000000 ) ) ;
#27607=AXIS2_PLACEMENT_3D ( 'NONE', #108409, #96825, #143226 ) ;
#27608=CARTESIAN_POINT ( 'NONE',  ( -2.999999999999977351, -15.03360074219758502, 5.000000000000000000 ) ) ;
#27609=VECTOR ( 'NONE', #42479, 1000.000000000000000 ) ;
#27610=ORIENTED_EDGE ( 'NONE', *, *, #3651, .F. ) ;
#27611=AXIS2_PLACEMENT_3D ( 'NONE', #31924, #110173, #110872 ) ;
#27612=FACE_OUTER_BOUND ( 'NONE', #57709, .T. ) ;
#27613=ORIENTED_EDGE ( 'NONE', *, *, #65135, .F. ) ;
#27614=ORIENTED_EDGE ( 'NONE', *, *, #85117, .F. ) ;
#27616=AXIS2_PLACEMENT_3D ( 'NONE', #129463, #22122, #74401 ) ;
#27617=CARTESIAN_POINT ( 'NONE',  ( -34.49999999999975131, -19.53574439159930876, 4.994342998332169437 ) ) ;
#27618=EDGE_CURVE ( 'NONE', #75984, #94048, #96382, .T. ) ;
#27620=DIRECTION ( 'NONE',  ( 0.6830127018922180770, -0.6830127018922204085, -0.2588190451025213501 ) ) ;
#27622=CARTESIAN_POINT ( 'NONE',  ( -10.49999999999992539, -20.53675388469231322, 2.352720554255868013 ) ) ;
#27623=VERTEX_POINT ( 'NONE', #41310 ) ;
#27625=PLANE ( 'NONE',  #32720 ) ;
#27627=CARTESIAN_POINT ( 'NONE',  ( -66.29974487139159578, -27.71228299555252406, 4.000000000000000000 ) ) ;
#27628=EDGE_CURVE ( 'NONE', #7053, #81238, #129755, .T. ) ;
#27629=LINE ( 'NONE', #105197, #16560 ) ;
#27632=CARTESIAN_POINT ( 'NONE',  ( 21.18398860626899349, 28.73617430169802134, 5.000000000000000000 ) ) ;
#27633=EDGE_LOOP ( 'NONE', ( #63830, #7601, #79392, #68573 ) ) ;
#27634=ORIENTED_EDGE ( 'NONE', *, *, #53003, .T. ) ;
#27635=ORIENTED_EDGE ( 'NONE', *, *, #113058, .T. ) ;
#27636=EDGE_CURVE ( 'NONE', #23479, #24882, #53641, .T. ) ;
#27638=ORIENTED_EDGE ( 'NONE', *, *, #9938, .T. ) ;
#27639=ORIENTED_EDGE ( 'NONE', *, *, #45037, .F. ) ;
#27640=ADVANCED_FACE ( 'NONE', ( #127630 ), #20986, .F. ) ;
#27641=ORIENTED_EDGE ( 'NONE', *, *, #131462, .F. ) ;
#27643=CARTESIAN_POINT ( 'NONE',  ( -30.70679250724055009, 20.25929247661551358, 20.83292124670821721 ) ) ;
#27644=ORIENTED_EDGE ( 'NONE', *, *, #44593, .F. ) ;
#27645=CARTESIAN_POINT ( 'NONE',  ( 2.343289998337851898, 3.759292476615681888, 13.27625715073266122 ) ) ;
#27646=EDGE_CURVE ( 'NONE', #14833, #16596, #112308, .T. ) ;
#27647=CARTESIAN_POINT ( 'NONE',  ( 0.3281693992235254487, 5.259292476615662792, 4.000000000000000000 ) ) ;
#27648=DIRECTION ( 'NONE',  ( -0.7071067811865487940, 0.7071067811865463515, 0.000000000000000000 ) ) ;
#27649=CARTESIAN_POINT ( 'NONE',  ( 0.000000000000000000, 0.000000000000000000, 5.000000000000000000 ) ) ;
#27652=CARTESIAN_POINT ( 'NONE',  ( 4.499999999999968914, 8.319652575858395238, -8.582050562765816792 ) ) ;
#27653=CARTESIAN_POINT ( 'NONE',  ( -5.292893218813418343, 20.25929247661551358, 5.000000000000000000 ) ) ;
#27655=CARTESIAN_POINT ( 'NONE',  ( -15.48921356237309510, -27.52281430457066236, 5.000000000000000000 ) ) ;
#27657=ADVANCED_FACE ( 'NONE', ( #100715 ), #12957, .F. ) ;
#27659=DIRECTION ( 'NONE',  ( -0.6830127018922180770, -0.6830127018922204085, -0.2588190451025213501 ) ) ;
#27661=DIRECTION ( 'NONE',  ( -0.7071067811865486830, -0.7071067811865464625, 0.000000000000000000 ) ) ;
#27663=VERTEX_POINT ( 'NONE', #32612 ) ;
#27664=ORIENTED_EDGE ( 'NONE', *, *, #84258, .T. ) ;
#27666=ORIENTED_EDGE ( 'NONE', *, *, #115171, .T. ) ;
#27667=EDGE_CURVE ( 'NONE', #132444, #10395, #110826, .T. ) ;
#27668=CARTESIAN_POINT ( 'NONE',  ( -27.18398860626900060, 28.73617430169806042, 5.000000000000000000 ) ) ;
#27670=ORIENTED_EDGE ( 'NONE', *, *, #112372, .T. ) ;
#27671=LINE ( 'NONE', #8729, #54947 ) ;
#27672=LINE ( 'NONE', #138602, #12145 ) ;
#27673=CARTESIAN_POINT ( 'NONE',  ( -33.48921356237309510, -27.52281430457078670, 5.000000000000000000 ) ) ;
#27674=LINE ( 'NONE', #62471, #14114 ) ;
#27676=EDGE_LOOP ( 'NONE', ( #29143, #128343, #38816, #118288, #106743 ) ) ;
#27677=CARTESIAN_POINT ( 'NONE',  ( 9.707106781186478628, -18.74070752338408496, 5.000000000000000000 ) ) ;
#27678=ORIENTED_EDGE ( 'NONE', *, *, #141668, .F. ) ;
#27681=VECTOR ( 'NONE', #132852, 1000.000000000000000 ) ;
#27682=VECTOR ( 'NONE', #47283, 1000.000000000000000 ) ;
#27683=CARTESIAN_POINT ( 'NONE',  ( -16.88982677111777875, -22.22500000000000142, 4.785647885939354751 ) ) ;
#27684=DIRECTION ( 'NONE',  ( -0.000000000000000000, -0.3543493200069152693, 0.9351131265310292928 ) ) ;
#27685=VECTOR ( 'NONE', #11296, 1000.000000000000000 ) ;
#27686=CARTESIAN_POINT ( 'NONE',  ( 0.000000000000000000, 0.000000000000000000, 5.000000000000000000 ) ) ;
#27687=ORIENTED_EDGE ( 'NONE', *, *, #120542, .T. ) ;
#27690=VERTEX_POINT ( 'NONE', #132661 ) ;
#27691=CARTESIAN_POINT ( 'NONE',  ( -26.51078643762690845, -27.52281430457036748, 5.000000000000000000 ) ) ;
#27692=CARTESIAN_POINT ( 'NONE',  ( 34.92382263987068569, 21.75929247661549937, 4.252424926123345550 ) ) ;
#27693=EDGE_CURVE ( 'NONE', #42437, #26598, #10806, .T. ) ;
#27694=LINE ( 'NONE', #5913, #87115 ) ;
#27695=CARTESIAN_POINT ( 'NONE',  ( -33.48921356237309510, -27.52281430457078670, 5.000000000000000000 ) ) ;
#27696=AXIS2_PLACEMENT_3D ( 'NONE', #102899, #57274, #68860 ) ;
#27697=ADVANCED_FACE ( 'NONE', ( #121719 ), #1359, .F. ) ;
#27698=VECTOR ( 'NONE', #113, 999.9999999999998863 ) ;
#27699=( BOUNDED_CURVE ( )  B_SPLINE_CURVE ( 3, ( #83104, #93965, #138923, #125903 ),
 .UNSPECIFIED., .F., .T. ) 
 B_SPLINE_CURVE_WITH_KNOTS ( ( 4, 4 ),
 ( 5.143245962375972091, 6.645403452391247079 ),
 .UNSPECIFIED. ) 
 CURVE ( )  GEOMETRIC_REPRESENTATION_ITEM ( )  RATIONAL_B_SPLINE_CURVE ( ( 1.000000000000000000, 0.8206354192515254997, 0.8206354192515254997, 1.000000000000000000 ) ) 
 REPRESENTATION_ITEM ( '' )  );
#27702=CARTESIAN_POINT ( 'NONE',  ( 20.20710678118640402, -20.24070752338407431, 5.000000000000000000 ) ) ;
#27703=LINE ( 'NONE', #125617, #94033 ) ;
#27704=EDGE_LOOP ( 'NONE', ( #22659, #18274, #87342 ) ) ;
#27705=EDGE_LOOP ( 'NONE', ( #87469, #463, #19680, #5954 ) ) ;
#27706=VECTOR ( 'NONE', #110353, 999.9999999999998863 ) ;
#27707=CARTESIAN_POINT ( 'NONE',  ( -14.67183060077637080, 8.259292476615636147, 4.000000000000000000 ) ) ;
#27708=EDGE_LOOP ( 'NONE', ( #2167, #110550, #19514, #73047 ) ) ;
#27709=EDGE_CURVE ( 'NONE', #107864, #43625, #76100, .T. ) ;
#27712=DIRECTION ( 'NONE',  ( -0.7071067811865486830, 0.7071067811865464625, 0.000000000000000000 ) ) ;
#27713=ORIENTED_EDGE ( 'NONE', *, *, #53457, .F. ) ;
#27715=VECTOR ( 'NONE', #31448, 1000.000000000000227 ) ;
#27716=VECTOR ( 'NONE', #75627, 1000.000000000000000 ) ;
#27717=CARTESIAN_POINT ( 'NONE',  ( -25.49999999999981881, -20.94781430457061333, 5.000000000000000000 ) ) ;
#27718=VECTOR ( 'NONE', #111443, 1000.000000000000000 ) ;
#27719=FACE_BOUND ( 'NONE', #25279, .T. ) ;
#27720=EDGE_CURVE ( 'NONE', #122403, #99882, #57231, .T. ) ;
#27721=CARTESIAN_POINT ( 'NONE',  ( 3.706123077391933140, 22.22500000000000142, 4.000000000000000000 ) ) ;
#27722=VECTOR ( 'NONE', #116591, 1000.000000000000000 ) ;
#27723=DIRECTION ( 'NONE',  ( -0.7071067811865486830, -0.7071067811865464625, 0.000000000000000000 ) ) ;
#27724=CARTESIAN_POINT ( 'NONE',  ( -81.29974487139159578, -27.71228299555262709, 4.000000000000000000 ) ) ;
#27725=AXIS2_PLACEMENT_3D ( 'NONE', #75490, #97954, #31279 ) ;
#27727=DIRECTION ( 'NONE',  ( 0.7071067811865487940, 0.7071067811865463515, 0.000000000000000000 ) ) ;
#27728=CYLINDRICAL_SURFACE ( 'NONE', #96880, 0.5000000000000004441 ) ;
#27729=ORIENTED_EDGE ( 'NONE', *, *, #58261, .T. ) ;
#27730=VECTOR ( 'NONE', #130018, 1000.000000000000000 ) ;
#27733=ORIENTED_EDGE ( 'NONE', *, *, #115798, .F. ) ;
#27736=ORIENTED_EDGE ( 'NONE', *, *, #19575, .T. ) ;
#27737=DIRECTION ( 'NONE',  ( 0.000000000000000000, -1.000000000000000000, 0.000000000000000000 ) ) ;
#27738=DIRECTION ( 'NONE',  ( -0.6830127018922180770, -0.6830127018922204085, -0.2588190451025213501 ) ) ;
#27739=VERTEX_POINT ( 'NONE', #142778 ) ;
#27740=CARTESIAN_POINT ( 'NONE',  ( -66.18398860626901126, 28.73617430169833753, 5.000000000000000000 ) ) ;
#27742=CARTESIAN_POINT ( 'NONE',  ( -12.52400138585440281, 22.03583458319438293, 4.979811245910087614 ) ) ;
#27743=DIRECTION ( 'NONE',  ( -0.000000000000000000, 0.000000000000000000, 1.000000000000000000 ) ) ;
#27744=DIRECTION ( 'NONE',  ( -0.7071067811865486830, -0.7071067811865464625, -0.000000000000000000 ) ) ;
#27745=DIRECTION ( 'NONE',  ( 0.7071067811865487940, -0.7071067811865463515, 0.000000000000000000 ) ) ;
#27746=VERTEX_POINT ( 'NONE', #11513 ) ;
#27747=EDGE_CURVE ( 'NONE', #26469, #32802, #661, .T. ) ;
#27748=AXIS2_PLACEMENT_3D ( 'NONE', #86623, #41666, #82504 ) ;
#27749=ORIENTED_EDGE ( 'NONE', *, *, #117963, .F. ) ;
#27751=FACE_OUTER_BOUND ( 'NONE', #92387, .T. ) ;
#27752=ORIENTED_EDGE ( 'NONE', *, *, #105978, .T. ) ;
#27753=ORIENTED_EDGE ( 'NONE', *, *, #11276, .T. ) ;
#27754=ORIENTED_EDGE ( 'NONE', *, *, #21616, .F. ) ;
#27755=DIRECTION ( 'NONE',  ( -0.6830127018922180770, -0.6830127018922204085, -0.2588190451025213501 ) ) ;
#27756=ADVANCED_FACE ( 'NONE', ( #123190 ), #87683, .F. ) ;
#27757=PLANE ( 'NONE',  #20742 ) ;
#27758=VERTEX_POINT ( 'NONE', #101407 ) ;
#27760=( BOUNDED_CURVE ( )  B_SPLINE_CURVE ( 3, ( #89527, #64940, #109134, #54089 ),
 .UNSPECIFIED., .F., .T. ) 
 B_SPLINE_CURVE_WITH_KNOTS ( ( 4, 4 ),
 ( 5.043186909253412509, 5.074607125596344304 ),
 .UNSPECIFIED. ) 
 CURVE ( )  GEOMETRIC_REPRESENTATION_ITEM ( )  RATIONAL_B_SPLINE_CURVE ( ( 1.000000000000000000, 0.9999177325257868620, 0.9999177325257868620, 1.000000000000000000 ) ) 
 REPRESENTATION_ITEM ( '' )  );
#27761=EDGE_CURVE ( 'NONE', #7238, #46933, #143483, .T. ) ;
#27762=DIRECTION ( 'NONE',  ( -0.6830127018922180770, -0.6830127018922204085, -0.2588190451025213501 ) ) ;
#27763=EDGE_CURVE ( 'NONE', #117341, #25152, #99998, .T. ) ;
#27764=ADVANCED_FACE ( 'NONE', ( #131916 ), #76844, .F. ) ;
#27766=FACE_OUTER_BOUND ( 'NONE', #51200, .T. ) ;
#27768=ORIENTED_EDGE ( 'NONE', *, *, #71170, .T. ) ;
#27769=EDGE_CURVE ( 'NONE', #133213, #64361, #90555, .T. ) ;
#27770=LINE ( 'NONE', #84332, #132237 ) ;
#27771=PLANE ( 'NONE',  #17364 ) ;
#27772=LINE ( 'NONE', #5982, #65736 ) ;
#27773=VERTEX_POINT ( 'NONE', #115102 ) ;
#27774=LINE ( 'NONE', #93037, #67979 ) ;
#27775=EDGE_LOOP ( 'NONE', ( #97098, #109204, #83985, #52209 ) ) ;
#27776=EDGE_CURVE ( 'NONE', #22900, #6599, #58690, .T. ) ;
#27777=CARTESIAN_POINT ( 'NONE',  ( -65.99451991528749772, 28.92564299267984396, 4.000000000000000000 ) ) ;
#27779=CARTESIAN_POINT ( 'NONE',  ( -34.92500000000001137, -13.48753812416036446, 4.000000000000000000 ) ) ;
#27780=EDGE_LOOP ( 'NONE', ( #32467, #122244, #113887, #74320 ) ) ;
#27781=EDGE_CURVE ( 'NONE', #61225, #73668, #80403, .T. ) ;
#27782=AXIS2_PLACEMENT_3D ( 'NONE', #2055, #36859, #48457 ) ;
#27783=CARTESIAN_POINT ( 'NONE',  ( 63.18398860626900415, 28.73617430169831621, 5.000000000000000000 ) ) ;
#27785=CARTESIAN_POINT ( 'NONE',  ( -4.499999999999966249, -8.947814304570732347, 5.000000000000000000 ) ) ;
#27786=ORIENTED_EDGE ( 'NONE', *, *, #72386, .F. ) ;
#27787=AXIS2_PLACEMENT_3D ( 'NONE', #116739, #97083, #29022 ) ;
#27788=VECTOR ( 'NONE', #98582, 999.9999999999998863 ) ;
#27790=PLANE ( 'NONE',  #18451 ) ;
#27791=CARTESIAN_POINT ( 'NONE',  ( -28.49999999999980105, 19.39370406404964697, 1.459788787078267092 ) ) ;
#27792=LINE ( 'NONE', #128545, #123420 ) ;
#27795=CARTESIAN_POINT ( 'NONE',  ( -21.16809626817622103, 8.755558144015518351, 4.000000000000000000 ) ) ;
#27796=ORIENTED_EDGE ( 'NONE', *, *, #36482, .T. ) ;
#27799=VECTOR ( 'NONE', #21429, 1000.000000000000227 ) ;
#27801=EDGE_CURVE ( 'NONE', #19828, #3251, #124597, .T. ) ;
#27803=CARTESIAN_POINT ( 'NONE',  ( 8.901564193917579360, 11.25929247661560595, 10.79108189686409069 ) ) ;
#27804=DIRECTION ( 'NONE',  ( -0.7071067811865486830, -0.7071067811865464625, 0.000000000000000000 ) ) ;
#27805=CARTESIAN_POINT ( 'NONE',  ( -34.42500000000001137, -22.22500000000000142, 5.000000000000000000 ) ) ;
#27806=FACE_OUTER_BOUND ( 'NONE', #122802, .T. ) ;
#27807=EDGE_LOOP ( 'NONE', ( #87421, #137769, #84567, #81035 ) ) ;
#27808=DIRECTION ( 'NONE',  ( 0.7071067811865487940, 0.7071067811865463515, 0.000000000000000000 ) ) ;
#27809=DIRECTION ( 'NONE',  ( -0.7071067811865486830, -0.7071067811865464625, 0.000000000000000000 ) ) ;
#27810=PLANE ( 'NONE',  #90948 ) ;
#27811=VECTOR ( 'NONE', #141949, 1000.000000000000227 ) ;
#27812=VECTOR ( 'NONE', #33242, 1000.000000000000000 ) ;
#27815=LINE ( 'NONE', #15475, #25644 ) ;
#27816=VECTOR ( 'NONE', #24991, 1000.000000000000000 ) ;
#27817=ORIENTED_EDGE ( 'NONE', *, *, #5014, .T. ) ;
#27819=ADVANCED_FACE ( 'NONE', ( #24563 ), #102859, .F. ) ;
#27821=EDGE_LOOP ( 'NONE', ( #122648, #53613, #64189, #4001 ) ) ;
#27822=DIRECTION ( 'NONE',  ( 0.000000000000000000, -0.000000000000000000, -1.000000000000000000 ) ) ;
#27823=VECTOR ( 'NONE', #52957, 1000.000000000000000 ) ;
#27824=EDGE_CURVE ( 'NONE', #133731, #8580, #57954, .T. ) ;
#27825=CARTESIAN_POINT ( 'NONE',  ( 45.18398860626900415, 28.73617430169818832, 5.000000000000000000 ) ) ;
#27826=DIRECTION ( 'NONE',  ( -0.000000000000000000, 0.000000000000000000, 1.000000000000000000 ) ) ;
#27827=DIRECTION ( 'NONE',  ( 0.6830127018922181881, 0.6830127018922202975, -0.2588190451025214056 ) ) ;
#27828=CARTESIAN_POINT ( 'NONE',  ( 18.32816939922339827, 14.25929247661557397, 4.000000000000000000 ) ) ;
#27830=VECTOR ( 'NONE', #79562, 999.9999999999998863 ) ;
#27831=ORIENTED_EDGE ( 'NONE', *, *, #35124, .F. ) ;
#27832=DIRECTION ( 'NONE',  ( -0.000000000000000000, -0.3543493200069152693, 0.9351131265310292928 ) ) ;
#27834=CARTESIAN_POINT ( 'NONE',  ( 19.82816939922339117, 12.75929247661558641, 4.000000000000000000 ) ) ;
#27835=LINE ( 'NONE', #3213, #116783 ) ;
#27836=EDGE_CURVE ( 'NONE', #90351, #118870, #102148, .T. ) ;
#27837=FACE_OUTER_BOUND ( 'NONE', #8447, .T. ) ;
#27839=DIRECTION ( 'NONE',  ( 0.6830127018922181881, 0.6830127018922202975, -0.2588190451025214056 ) ) ;
#27841=ORIENTED_EDGE ( 'NONE', *, *, #75179, .T. ) ;
#27844=DIRECTION ( 'NONE',  ( 0.3543493200069163240, 0.000000000000000000, -0.9351131265310288487 ) ) ;
#27845=ADVANCED_FACE ( 'NONE', ( #48461 ), #70949, .F. ) ;
#27846=CARTESIAN_POINT ( 'NONE',  ( 12.70710678118645198, 17.25929247661553489, 5.000000000000000000 ) ) ;
#27847=VECTOR ( 'NONE', #139490, 1000.000000000000000 ) ;
#27848=ORIENTED_EDGE ( 'NONE', *, *, #131131, .T. ) ;
#27849=LINE ( 'NONE', #6058, #102315 ) ;
#27850=CARTESIAN_POINT ( 'NONE',  ( 1.001930566820972812, -22.22500000000000142, 4.500000000000000888 ) ) ;
#27852=DIRECTION ( 'NONE',  ( -0.7071067811865487940, 0.7071067811865463515, -0.000000000000000000 ) ) ;
#27853=ORIENTED_EDGE ( 'NONE', *, *, #73623, .F. ) ;
#27855=AXIS2_PLACEMENT_3D ( 'NONE', #121019, #44952, #89131 ) ;
#27856=DIRECTION ( 'NONE',  ( -0.000000000000000000, 0.000000000000000000, 1.000000000000000000 ) ) ;
#27857=DIRECTION ( 'NONE',  ( 0.3543493200069162685, -0.000000000000000000, -0.9351131265310288487 ) ) ;
#27858=CARTESIAN_POINT ( 'NONE',  ( 24.18398860626899705, 28.73617430169804265, 5.000000000000000000 ) ) ;
#27860=EDGE_CURVE ( 'NONE', #35758, #100009, #91960, .T. ) ;
#27861=LINE ( 'NONE', #103969, #127573 ) ;
#27863=ORIENTED_EDGE ( 'NONE', *, *, #9944, .T. ) ;
#27864=EDGE_CURVE ( 'NONE', #25222, #32191, #103529, .T. ) ;
#27866=CARTESIAN_POINT ( 'NONE',  ( -2.510786437626908008, -27.52281430457053446, 5.000000000000000000 ) ) ;
#27867=DIRECTION ( 'NONE',  ( 0.7071067811865487940, 0.7071067811865463515, 0.000000000000000000 ) ) ;
#27868=VECTOR ( 'NONE', #22104, 1000.000000000000000 ) ;
#27869=CARTESIAN_POINT ( 'NONE',  ( 33.48921356237309510, -27.52281430457078670, 5.000000000000000000 ) ) ;
#27871=ORIENTED_EDGE ( 'NONE', *, *, #427, .F. ) ;
#27872=CARTESIAN_POINT ( 'NONE',  ( -81.18398860626899705, 28.73617430169844056, 5.000000000000000000 ) ) ;
#27873=DIRECTION ( 'NONE',  ( 0.7071067811865486830, -0.7071067811865464625, -0.000000000000000000 ) ) ;
#27874=DIRECTION ( 'NONE',  ( 0.7071067811865487940, 0.7071067811865463515, -0.000000000000000000 ) ) ;
#27876=DIRECTION ( 'NONE',  ( -0.6830127018922180770, -0.6830127018922204085, -0.2588190451025213501 ) ) ;
#27879=FACE_OUTER_BOUND ( 'NONE', #66074, .T. ) ;
#27881=AXIS2_PLACEMENT_3D ( 'NONE', #35160, #79402, #68505 ) ;
#27882=VERTEX_POINT ( 'NONE', #81847 ) ;
#27883=EDGE_CURVE ( 'NONE', #94410, #83442, #126040, .T. ) ;
#27884=VECTOR ( 'NONE', #23821, 1000.000000000000000 ) ;
#27886=EDGE_LOOP ( 'NONE', ( #66439, #26342, #139504, #39256 ) ) ;
#27888=FACE_OUTER_BOUND ( 'NONE', #98271, .T. ) ;
#27889=ORIENTED_EDGE ( 'NONE', *, *, #37604, .F. ) ;
#27891=CARTESIAN_POINT ( 'NONE',  ( 8.994519915287490619, 28.92564299267944250, 4.000000000000000000 ) ) ;
#27892=VECTOR ( 'NONE', #46217, 1000.000000000000000 ) ;
#27896=FACE_BOUND ( 'NONE', #52513, .T. ) ;
#27899=FACE_OUTER_BOUND ( 'NONE', #48277, .T. ) ;
#27900=VECTOR ( 'NONE', #15849, 1000.000000000000000 ) ;
#27901=DIRECTION ( 'NONE',  ( -0.7071067811865486830, -0.7071067811865464625, -0.000000000000000000 ) ) ;
#27903=LINE ( 'NONE', #16276, #6991 ) ;
#27906=VERTEX_POINT ( 'NONE', #117958 ) ;
#27908=ORIENTED_EDGE ( 'NONE', *, *, #105476, .F. ) ;
#27909=CARTESIAN_POINT ( 'NONE',  ( -24.18398860626899705, 28.73617430169804265, 5.000000000000000000 ) ) ;
#27910=VECTOR ( 'NONE', #40490, 999.9999999999998863 ) ;
#27912=DIRECTION ( 'NONE',  ( -0.000000000000000000, -0.3543493200069152693, 0.9351131265310292928 ) ) ;
#27913=AXIS2_PLACEMENT_3D ( 'NONE', #42166, #117532, #97196 ) ;
#27915=EDGE_LOOP ( 'NONE', ( #40340, #77604, #27359, #128660, #31298 ) ) ;
#27916=LINE ( 'NONE', #48976, #73849 ) ;
#27918=DIRECTION ( 'NONE',  ( -0.000000000000000000, 0.3543493200069153248, 0.9351131265310292928 ) ) ;
#27919=CARTESIAN_POINT ( 'NONE',  ( 21.71230993966012690, -21.73547319004781997, 4.999917730833664642 ) ) ;
#27920=CARTESIAN_POINT ( 'NONE',  ( -19.05000000000000071, 3.174999999999997158, 4.000000000000000000 ) ) ;
#27921=CARTESIAN_POINT ( 'NONE',  ( -27.48921356237309155, -27.52281430457074762, 5.000000000000000000 ) ) ;
#27922=VECTOR ( 'NONE', #64040, 1000.000000000000000 ) ;
#27923=DIRECTION ( 'NONE',  ( 0.7071067811865486830, -0.7071067811865464625, -0.000000000000000000 ) ) ;
#27924=DIRECTION ( 'NONE',  ( -0.6830127018922180770, -0.6830127018922204085, -0.2588190451025213501 ) ) ;
#27926=LINE ( 'NONE', #117752, #134850 ) ;
#27929=CARTESIAN_POINT ( 'NONE',  ( 2.999999999999985345, -16.06887692260765377, 4.000000000000000000 ) ) ;
#27930=DIRECTION ( 'NONE',  ( -0.7071067811865486830, -0.7071067811865464625, 0.000000000000000000 ) ) ;
#27931=ORIENTED_EDGE ( 'NONE', *, *, #14153, .F. ) ;
#27932=ORIENTED_EDGE ( 'NONE', *, *, #63023, .F. ) ;
#27933=VECTOR ( 'NONE', #49603, 1000.000000000000227 ) ;
#27934=EDGE_LOOP ( 'NONE', ( #59810, #46466, #132654, #122599 ) ) ;
#27936=VERTEX_POINT ( 'NONE', #120842 ) ;
#27937=ADVANCED_FACE ( 'NONE', ( #32430 ), #33864, .T. ) ;
#27940=EDGE_CURVE ( 'NONE', #18168, #137344, #43308, .T. ) ;
#27941=ORIENTED_EDGE ( 'NONE', *, *, #113793, .F. ) ;
#27942=ADVANCED_FACE ( 'NONE', ( #65074 ), #78082, .F. ) ;
#27943=CARTESIAN_POINT ( 'NONE',  ( -8.816011393731004731, 28.73617430169781173, 5.000000000000000000 ) ) ;
#27944=EDGE_CURVE ( 'NONE', #55527, #20152, #126759, .T. ) ;
#27946=CARTESIAN_POINT ( 'NONE',  ( 18.75860074219783868, 21.72500000000000853, 5.000000000000000000 ) ) ;
#27948=CARTESIAN_POINT ( 'NONE',  ( -34.92500000000001137, -22.22500000000000142, 4.000000000000000000 ) ) ;
#27949=CARTESIAN_POINT ( 'NONE',  ( 28.49999999999981171, -4.912538124160708897, 4.000000000000000000 ) ) ;
#27950=ORIENTED_EDGE ( 'NONE', *, *, #86033, .F. ) ;
#27952=EDGE_CURVE ( 'NONE', #23925, #133903, #55614, .T. ) ;
#27953=DIRECTION ( 'NONE',  ( 0.6830127018922181881, 0.6830127018922202975, -0.2588190451025214056 ) ) ;
#27955=ORIENTED_EDGE ( 'NONE', *, *, #125969, .T. ) ;
#27956=LINE ( 'NONE', #6870, #129192 ) ;
#27957=ORIENTED_EDGE ( 'NONE', *, *, #89336, .F. ) ;
#27958=VERTEX_POINT ( 'NONE', #481 ) ;
#27959=ORIENTED_EDGE ( 'NONE', *, *, #5979, .T. ) ;
#27960=EDGE_CURVE ( 'NONE', #81752, #112523, #1189, .T. ) ;
#27961=VERTEX_POINT ( 'NONE', #34569 ) ;
#27962=PLANE ( 'NONE',  #30873 ) ;
#27963=AXIS2_PLACEMENT_3D ( 'NONE', #62759, #138892, #128707 ) ;
#27965=EDGE_CURVE ( 'NONE', #46724, #104812, #44020, .T. ) ;
#27966=FACE_OUTER_BOUND ( 'NONE', #139332, .T. ) ;
#27968=ADVANCED_FACE ( 'NONE', ( #88239 ), #10638, .F. ) ;
#27969=ORIENTED_EDGE ( 'NONE', *, *, #96630, .T. ) ;
#27971=ORIENTED_EDGE ( 'NONE', *, *, #35581, .F. ) ;
#27972=VECTOR ( 'NONE', #7487, 1000.000000000000000 ) ;
#27973=CARTESIAN_POINT ( 'NONE',  ( -36.48921356237310221, -27.52281430457080802, 5.000000000000000000 ) ) ;
#27974=EDGE_CURVE ( 'NONE', #358, #90591, #122257, .T. ) ;
#27976=PLANE ( 'NONE',  #122672 ) ;
#27977=DIRECTION ( 'NONE',  ( 0.7071067811865487940, -0.7071067811865463515, 0.000000000000000000 ) ) ;
#27979=ORIENTED_EDGE ( 'NONE', *, *, #65956, .T. ) ;
#27980=ORIENTED_EDGE ( 'NONE', *, *, #47335, .T. ) ;
#27981=ORIENTED_EDGE ( 'NONE', *, *, #12367, .F. ) ;
#27982=CARTESIAN_POINT ( 'NONE',  ( -26.99451991528749417, 28.92564299267956685, 4.000000000000000000 ) ) ;
#27983=CARTESIAN_POINT ( 'NONE',  ( 34.49999999999975842, 18.43112307739199451, 4.000000000000000000 ) ) ;
#27984=DIRECTION ( 'NONE',  ( -0.7071067811865486830, 0.7071067811865464625, 0.000000000000000000 ) ) ;
#27986=VECTOR ( 'NONE', #111241, 1000.000000000000000 ) ;
#27989=( BOUNDED_CURVE ( )  B_SPLINE_CURVE ( 3, ( #136800, #126617, #27309, #71561 ),
 .UNSPECIFIED., .F., .F. ) 
 B_SPLINE_CURVE_WITH_KNOTS ( ( 4, 4 ),
 ( 1.964434688349492752, 3.503810798801450854 ),
 .UNSPECIFIED. ) 
 CURVE ( )  GEOMETRIC_REPRESENTATION_ITEM ( )  RATIONAL_B_SPLINE_CURVE ( ( 1.000000000000000000, 0.8120851936182292841, 0.8120851936182292841, 1.000000000000000000 ) ) 
 REPRESENTATION_ITEM ( '' )  );
#27990=DIRECTION ( 'NONE',  ( -0.7071067811865487940, 0.7071067811865463515, 0.000000000000000000 ) ) ;
#27991=VECTOR ( 'NONE', #9147, 1000.000000000000000 ) ;
#27992=VECTOR ( 'NONE', #49139, 1000.000000000000000 ) ;
#27993=LINE ( 'NONE', #17117, #85450 ) ;
#27994=PLANE ( 'NONE',  #95812 ) ;
#27996=CARTESIAN_POINT ( 'NONE',  ( -34.42500000000001137, -21.72500000000000142, 0.5000000000000000000 ) ) ;
#27997=ADVANCED_FACE ( 'NONE', ( #123006 ), #66492, .T. ) ;
#27998=VERTEX_POINT ( 'NONE', #120102 ) ;
#27999=VECTOR ( 'NONE', #78442, 1000.000000000000227 ) ;
#28000=AXIS2_PLACEMENT_3D ( 'NONE', #47494, #36558, #124999 ) ;
#28002=CARTESIAN_POINT ( 'NONE',  ( 7.171830600776418763, -2.240707523384260824, 4.000000000000000000 ) ) ;
#28003=ORIENTED_EDGE ( 'NONE', *, *, #70732, .T. ) ;
#28005=CARTESIAN_POINT ( 'NONE',  ( 13.49999999999990052, -9.462702396501002866, -9.474982329943548720 ) ) ;
#28006=LINE ( 'NONE', #83101, #64966 ) ;
#28008=FACE_OUTER_BOUND ( 'NONE', #93814, .T. ) ;
#28009=LINE ( 'NONE', #59245, #40284 ) ;
#28010=ORIENTED_EDGE ( 'NONE', *, *, #19829, .F. ) ;
#28012=PLANE ( 'NONE',  #30419 ) ;
#28013=VECTOR ( 'NONE', #55687, 1000.000000000000000 ) ;
#28014=ORIENTED_EDGE ( 'NONE', *, *, #19785, .F. ) ;
#28015=DIRECTION ( 'NONE',  ( -0.7071067811865486830, -0.7071067811865464625, 0.000000000000000000 ) ) ;
#28018=DIRECTION ( 'NONE',  ( 0.6830127018922181881, 0.6830127018922202975, -0.2588190451025214056 ) ) ;
#28020=ORIENTED_EDGE ( 'NONE', *, *, #138465, .F. ) ;
#28021=VECTOR ( 'NONE', #13250, 1000.000000000000000 ) ;
#28022=PLANE ( 'NONE',  #14494 ) ;
#28023=EDGE_CURVE ( 'NONE', #57534, #113103, #131745, .T. ) ;
#28026=DIRECTION ( 'NONE',  ( -0.7071067811865486830, -0.7071067811865464625, 0.000000000000000000 ) ) ;
#28027=DIRECTION ( 'NONE',  ( -0.7071067811865487940, 0.7071067811865463515, -0.000000000000000000 ) ) ;
#28029=VECTOR ( 'NONE', #3782, 999.9999999999998863 ) ;
#28031=EDGE_LOOP ( 'NONE', ( #137315, #16031 ) ) ;
#28033=EDGE_CURVE ( 'NONE', #13955, #4136, #141925, .T. ) ;
#28036=DIRECTION ( 'NONE',  ( -0.000000000000000000, -0.3543493200069152693, 0.9351131265310292928 ) ) ;
#28037=CARTESIAN_POINT ( 'NONE',  ( 34.42499999999998295, 19.54139925780185294, 5.000000000000000000 ) ) ;
#28039=VERTEX_POINT ( 'NONE', #109260 ) ;
#28040=VECTOR ( 'NONE', #29077, 1000.000000000000000 ) ;
#28041=PLANE ( 'NONE',  #53516 ) ;
#28044=EDGE_CURVE ( 'NONE', #8196, #39664, #54905, .T. ) ;
#28045=VECTOR ( 'NONE', #60296, 1000.000000000000000 ) ;
#28046=DIRECTION ( 'NONE',  ( -0.6830127018922181881, 0.6830127018922202975, -0.2588190451025214056 ) ) ;
#28047=VERTEX_POINT ( 'NONE', #76669 ) ;
#28049=CARTESIAN_POINT ( 'NONE',  ( -34.92500000000001137, 2.816654386410402555, 4.500000000000000888 ) ) ;
#28050=PLANE ( 'NONE',  #70238 ) ;
#28052=ORIENTED_EDGE ( 'NONE', *, *, #135880, .F. ) ;
#28053=EDGE_LOOP ( 'NONE', ( #96545, #12561, #36367, #53262 ) ) ;
#28056=ORIENTED_EDGE ( 'NONE', *, *, #89094, .T. ) ;
#28059=LINE ( 'NONE', #125230, #66539 ) ;
#28060=CARTESIAN_POINT ( 'NONE',  ( 26.99999999999981526, -1.068876922607795654, 4.000000000000000000 ) ) ;
#28061=VERTEX_POINT ( 'NONE', #98398 ) ;
#28062=CARTESIAN_POINT ( 'NONE',  ( 51.29974487139158867, -27.71228299555242103, 4.000000000000000000 ) ) ;
#28064=VERTEX_POINT ( 'NONE', #142618 ) ;
#28065=EDGE_CURVE ( 'NONE', #83610, #88267, #121554, .T. ) ;
#28067=LINE ( 'NONE', #26637, #47922 ) ;
#28068=CARTESIAN_POINT ( 'NONE',  ( 36.18398860626899705, 28.73617430169812437, 5.000000000000000000 ) ) ;
#28070=EDGE_LOOP ( 'NONE', ( #12400, #80896, #141579, #127451 ) ) ;
#28072=EDGE_CURVE ( 'NONE', #47652, #143140, #2624, .T. ) ;
#28073=EDGE_CURVE ( 'NONE', #42777, #82100, #70097, .T. ) ;
#28075=LINE ( 'NONE', #72342, #64734 ) ;
#28077=CARTESIAN_POINT ( 'NONE',  ( -9.328169399223467551, 14.25929247661557397, 4.000000000000000000 ) ) ;
#28078=AXIS2_PLACEMENT_3D ( 'NONE', #122508, #132729, #78317 ) ;
#28079=DIRECTION ( 'NONE',  ( 0.3543493200069162685, -0.000000000000000000, -0.9351131265310288487 ) ) ;
#28081=VERTEX_POINT ( 'NONE', #23682 ) ;
#28082=ORIENTED_EDGE ( 'NONE', *, *, #57353, .T. ) ;
#28083=ORIENTED_EDGE ( 'NONE', *, *, #73695, .F. ) ;
#28084=ORIENTED_EDGE ( 'NONE', *, *, #102283, .T. ) ;
#28086=EDGE_CURVE ( 'NONE', #62473, #72185, #136716, .T. ) ;
#28087=LINE ( 'NONE', #139003, #61770 ) ;
#28089=VECTOR ( 'NONE', #104742, 1000.000000000000114 ) ;
#28090=ORIENTED_EDGE ( 'NONE', *, *, #64767, .F. ) ;
#28091=FACE_OUTER_BOUND ( 'NONE', #74963, .T. ) ;
#28092=CARTESIAN_POINT ( 'NONE',  ( -5.999999999999954703, -9.033600742197647193, 5.000000000000000000 ) ) ;
#28093=FACE_OUTER_BOUND ( 'NONE', #106651, .T. ) ;
#28094=CARTESIAN_POINT ( 'NONE',  ( -39.29974487139159578, -27.71228299555233576, 4.000000000000000000 ) ) ;
#28095=VECTOR ( 'NONE', #130378, 1000.000000000000000 ) ;
#28096=AXIS2_PLACEMENT_3D ( 'NONE', #142650, #65112, #86850 ) ;
#28098=CARTESIAN_POINT ( 'NONE',  ( 0.000000000000000000, 0.000000000000000000, 5.000000000000000000 ) ) ;
#28099=ORIENTED_EDGE ( 'NONE', *, *, #39600, .F. ) ;
#28100=VECTOR ( 'NONE', #91608, 999.9999999999998863 ) ;
#28101=CARTESIAN_POINT ( 'NONE',  ( -34.92500000000001137, -10.48753812416038933, 4.000000000000000000 ) ) ;
#28102=LINE ( 'NONE', #6287, #85935 ) ;
#28103=ORIENTED_EDGE ( 'NONE', *, *, #749, .F. ) ;
#28104=PLANE ( 'NONE',  #66629 ) ;
#28105=VERTEX_POINT ( 'NONE', #59210 ) ;
#28106=ORIENTED_EDGE ( 'NONE', *, *, #56488, .T. ) ;
#28107=LINE ( 'NONE', #85319, #108479 ) ;
#28108=VERTEX_POINT ( 'NONE', #13488 ) ;
#28109=ORIENTED_EDGE ( 'NONE', *, *, #111355, .T. ) ;
#28110=EDGE_CURVE ( 'NONE', #23291, #27437, #125872, .T. ) ;
#28113=VERTEX_POINT ( 'NONE', #37427 ) ;
#28114=LINE ( 'NONE', #61493, #67491 ) ;
#28115=EDGE_CURVE ( 'NONE', #97839, #54633, #93221, .T. ) ;
#28118=CARTESIAN_POINT ( 'NONE',  ( 21.29974487139158512, -27.71228299555221142, 4.000000000000000000 ) ) ;
#28119=VECTOR ( 'NONE', #97428, 1000.000000000000000 ) ;
#28120=ADVANCED_FACE ( 'NONE', ( #124423 ), #113529, .F. ) ;
#28121=FACE_OUTER_BOUND ( 'NONE', #55710, .T. ) ;
#28122=CARTESIAN_POINT ( 'NONE',  ( -25.63753812416080180, 22.22500000000000142, 4.000000000000000000 ) ) ;
#28123=CARTESIAN_POINT ( 'NONE',  ( 13.49999999999991118, -2.568876922607790103, 4.000000000000000000 ) ) ;
#28124=EDGE_CURVE ( 'NONE', #21745, #123150, #24393, .T. ) ;
#28125=ADVANCED_FACE ( 'NONE', ( #79549 ), #70785, .F. ) ;
#28127=AXIS2_PLACEMENT_3D ( 'NONE', #5041, #2184, #57355 ) ;
#28129=EDGE_LOOP ( 'NONE', ( #47210, #5079, #17635, #23284 ) ) ;
#28130=VECTOR ( 'NONE', #68058, 1000.000000000000000 ) ;
#28131=ORIENTED_EDGE ( 'NONE', *, *, #45682, .T. ) ;
#28133=VERTEX_POINT ( 'NONE', #14231 ) ;
#28134=CARTESIAN_POINT ( 'NONE',  ( 14.99999999999989875, 17.58746187583906462, 4.000000000000000000 ) ) ;
#28136=VECTOR ( 'NONE', #91333, 1000.000000000000227 ) ;
#28137=DIRECTION ( 'NONE',  ( 0.3543493200069162685, -0.000000000000000000, -0.9351131265310288487 ) ) ;
#28140=VECTOR ( 'NONE', #142498, 1000.000000000000227 ) ;
#28142=ADVANCED_FACE ( 'NONE', ( #92489 ), #46926, .F. ) ;
#28143=LINE ( 'NONE', #122823, #106497 ) ;
#28145=EDGE_LOOP ( 'NONE', ( #100535, #27517, #75599, #56640 ) ) ;
#28146=ORIENTED_EDGE ( 'NONE', *, *, #123833, .F. ) ;
#28147=ADVANCED_FACE ( 'NONE', ( #4010 ), #48289, .F. ) ;
#28149=DIRECTION ( 'NONE',  ( 0.7071067811865486830, -0.7071067811865464625, -0.000000000000000000 ) ) ;
#28150=DIRECTION ( 'NONE',  ( -0.7071067811865487940, 0.7071067811865463515, -0.000000000000000000 ) ) ;
#28151=DIRECTION ( 'NONE',  ( 0.6830127018922181881, 0.6830127018922202975, -0.2588190451025214056 ) ) ;
#28153=EDGE_LOOP ( 'NONE', ( #62439, #19044, #25780, #142894 ) ) ;
#28155=ORIENTED_EDGE ( 'NONE', *, *, #64017, .T. ) ;
#28157=FACE_OUTER_BOUND ( 'NONE', #96031, .T. ) ;
#28158=ADVANCED_FACE ( 'NONE', ( #114932 ), #90361, .T. ) ;
#28159=CARTESIAN_POINT ( 'NONE',  ( 26.99451991528749417, 28.92564299267956685, 4.000000000000000000 ) ) ;
#28160=AXIS2_PLACEMENT_3D ( 'NONE', #76149, #120314, #139997 ) ;
#28161=PLANE ( 'NONE',  #106407 ) ;
#28162=DIRECTION ( 'NONE',  ( 0.6830127018922181881, 0.6830127018922202975, -0.2588190451025214056 ) ) ;
#28163=LINE ( 'NONE', #72424, #27722 ) ;
#28164=CARTESIAN_POINT ( 'NONE',  ( 11.99999999999991651, 19.55218569542897100, 5.000000000000000000 ) ) ;
#28166=ORIENTED_EDGE ( 'NONE', *, *, #60540, .T. ) ;
#28168=EDGE_CURVE ( 'NONE', #75175, #59824, #15610, .T. ) ;
#28169=AXIS2_PLACEMENT_3D ( 'NONE', #73987, #8669, #7984 ) ;
#28170=CARTESIAN_POINT ( 'NONE',  ( -9.812461875839401770, -22.22500000000000142, 4.000000000000000000 ) ) ;
#28171=ORIENTED_EDGE ( 'NONE', *, *, #10881, .F. ) ;
#28172=DIRECTION ( 'NONE',  ( -0.7071067811865487940, 0.7071067811865463515, 0.000000000000000000 ) ) ;
#28175=DIRECTION ( 'NONE',  ( 0.000000000000000000, -1.000000000000000000, 0.000000000000000000 ) ) ;
#28176=EDGE_CURVE ( 'NONE', #49695, #68309, #91786, .T. ) ;
#28178=EDGE_CURVE ( 'NONE', #139670, #70176, #59897, .T. ) ;
#28179=VECTOR ( 'NONE', #94518, 1000.000000000000000 ) ;
#28180=EDGE_LOOP ( 'NONE', ( #66642, #76843, #57562, #129584 ) ) ;
#28181=FACE_OUTER_BOUND ( 'NONE', #75709, .T. ) ;
#28182=ORIENTED_EDGE ( 'NONE', *, *, #13763, .T. ) ;
#28183=( BOUNDED_CURVE ( )  B_SPLINE_CURVE ( 3, ( #12861, #76004, #142689, #86889 ),
 .UNSPECIFIED., .F., .T. ) 
 B_SPLINE_CURVE_WITH_KNOTS ( ( 4, 4 ),
 ( 4.350170835173036821, 4.500739107949268458 ),
 .UNSPECIFIED. ) 
 CURVE ( )  GEOMETRIC_REPRESENTATION_ITEM ( )  RATIONAL_B_SPLINE_CURVE ( ( 1.000000000000000000, 0.9981116584018945304, 0.9981116584018945304, 1.000000000000000000 ) ) 
 REPRESENTATION_ITEM ( '' )  );
#28184=DIRECTION ( 'NONE',  ( -0.6830127018922180770, -0.6830127018922204085, -0.2588190451025213501 ) ) ;
#28185=EDGE_CURVE ( 'NONE', #25281, #50352, #112137, .T. ) ;
#28187=DIRECTION ( 'NONE',  ( 0.6830127018922180770, -0.6830127018922204085, -0.2588190451025213501 ) ) ;
#28188=FACE_OUTER_BOUND ( 'NONE', #61012, .T. ) ;
#28189=CARTESIAN_POINT ( 'NONE',  ( -15.48921356237309510, -27.52281430457066236, 5.000000000000000000 ) ) ;
#28190=CARTESIAN_POINT ( 'NONE',  ( 39.48921356237310221, -27.52281430457082934, 5.000000000000000000 ) ) ;
#28191=PLANE ( 'NONE',  #43675 ) ;
#28194=LINE ( 'NONE', #141792, #129228 ) ;
#28195=AXIS2_PLACEMENT_3D ( 'NONE', #120673, #131583, #107667 ) ;
#28197=CARTESIAN_POINT ( 'NONE',  ( 7.226741607178295723, -11.24070752338416135, 18.24660765846983779 ) ) ;
#28198=DIRECTION ( 'NONE',  ( 0.7071067811865487940, 0.7071067811865463515, 0.000000000000000000 ) ) ;
#28199=ORIENTED_EDGE ( 'NONE', *, *, #49349, .T. ) ;
#28200=EDGE_LOOP ( 'NONE', ( #11947, #62410, #114500 ) ) ;
#28201=VECTOR ( 'NONE', #60057, 999.9999999999998863 ) ;
#28203=VECTOR ( 'NONE', #116164, 999.9999999999998863 ) ;
#28205=ORIENTED_EDGE ( 'NONE', *, *, #36474, .T. ) ;
#28210=DIRECTION ( 'NONE',  ( 0.7071067811865487940, -0.7071067811865463515, 0.000000000000000000 ) ) ;
#28211=EDGE_LOOP ( 'NONE', ( #110566, #41433, #55263, #101001 ) ) ;
#28212=VECTOR ( 'NONE', #99322, 1000.000000000000000 ) ;
#28213=CARTESIAN_POINT ( 'NONE',  ( -36.29974487139159578, -27.71228299555231445, 4.000000000000000000 ) ) ;
#28214=CARTESIAN_POINT ( 'NONE',  ( 48.29974487139158867, -27.71228299555239971, 4.000000000000000000 ) ) ;
#28215=DIRECTION ( 'NONE',  ( 0.7071067811865487940, 0.7071067811865463515, 0.000000000000000000 ) ) ;
#28217=DIRECTION ( 'NONE',  ( -0.7071067811865486830, -0.7071067811865464625, 0.000000000000000000 ) ) ;
#28218=LINE ( 'NONE', #83316, #112343 ) ;
#28221=CARTESIAN_POINT ( 'NONE',  ( -24.48921356237309510, -27.52281430457072631, 5.000000000000000000 ) ) ;
#28222=LINE ( 'NONE', #5716, #95633 ) ;
#28223=DIRECTION ( 'NONE',  ( -0.7071067811865486830, -0.7071067811865463515, 0.000000000000000000 ) ) ;
#28224=DIRECTION ( 'NONE',  ( 0.7071067811865487940, 0.7071067811865463515, 0.000000000000000000 ) ) ;
#28226=ORIENTED_EDGE ( 'NONE', *, *, #87652, .T. ) ;
#28227=ORIENTED_EDGE ( 'NONE', *, *, #94146, .T. ) ;
#28229=EDGE_LOOP ( 'NONE', ( #100723, #102779, #53041, #20585 ) ) ;
#28231=CARTESIAN_POINT ( 'NONE',  ( -13.49999999999988987, 19.08746187583904330, 4.000000000000000000 ) ) ;
#28233=CARTESIAN_POINT ( 'NONE',  ( -34.82816939922328459, -8.240707523384189770, 4.000000000000000000 ) ) ;
#28234=PLANE ( 'NONE',  #92870 ) ;
#28235=AXIS2_PLACEMENT_3D ( 'NONE', #113668, #15056, #25958 ) ;
#28238=VERTEX_POINT ( 'NONE', #35309 ) ;
#28240=CARTESIAN_POINT ( 'NONE',  ( 5.700255128608413102, -27.71228299555201957, 4.000000000000000000 ) ) ;
#28241=ORIENTED_EDGE ( 'NONE', *, *, #23223, .T. ) ;
#28243=LINE ( 'NONE', #95625, #127943 ) ;
#28244=VECTOR ( 'NONE', #93657, 1000.000000000000000 ) ;
#28245=DIRECTION ( 'NONE',  ( -0.7071067811865486830, -0.7071067811865464625, 0.000000000000000000 ) ) ;
#28246=CARTESIAN_POINT ( 'NONE',  ( 16.36246187583891754, 22.22499999999999432, 4.000000000000000000 ) ) ;
#28247=ORIENTED_EDGE ( 'NONE', *, *, #67840, .F. ) ;
#28248=ORIENTED_EDGE ( 'NONE', *, *, #49978, .F. ) ;
#28249=EDGE_CURVE ( 'NONE', #94548, #64904, #40991, .T. ) ;
#28250=ORIENTED_EDGE ( 'NONE', *, *, #49810, .F. ) ;
#28252=EDGE_CURVE ( 'NONE', #94631, #103858, #28704, .T. ) ;
#28253=FACE_OUTER_BOUND ( 'NONE', #90726, .T. ) ;
#28256=LINE ( 'NONE', #85460, #20124 ) ;
#28257=DIRECTION ( 'NONE',  ( -0.3543493200069162685, -0.000000000000000000, -0.9351131265310288487 ) ) ;
#28258=VERTEX_POINT ( 'NONE', #116408 ) ;
#28259=EDGE_CURVE ( 'NONE', #117324, #53860, #96750, .T. ) ;
#28260=ORIENTED_EDGE ( 'NONE', *, *, #137131, .T. ) ;
#28261=CARTESIAN_POINT ( 'NONE',  ( 20.99999999999985789, -19.44781430457063465, 5.000000000000000000 ) ) ;
#28263=VERTEX_POINT ( 'NONE', #63491 ) ;
#28264=VECTOR ( 'NONE', #68737, 1000.000000000000114 ) ;
#28265=AXIS2_PLACEMENT_3D ( 'NONE', #97717, #141969, #17978 ) ;
#28267=EDGE_CURVE ( 'NONE', #28405, #81467, #72948, .T. ) ;
#28269=CARTESIAN_POINT ( 'NONE',  ( -21.18398860626899349, 28.73617430169802134, 5.000000000000000000 ) ) ;
#28270=EDGE_LOOP ( 'NONE', ( #47949, #72683, #14178, #39552 ) ) ;
#28271=CARTESIAN_POINT ( 'NONE',  ( 21.42327845806341102, 11.25929247661560240, 17.85071094206579545 ) ) ;
#28272=CARTESIAN_POINT ( 'NONE',  ( -20.70025512860841133, -27.71228299555191654, 4.000000000000000000 ) ) ;
#28273=DIRECTION ( 'NONE',  ( -0.7071067811865486830, 0.7071067811865464625, 0.000000000000000000 ) ) ;
#28274=EDGE_CURVE ( 'NONE', #44583, #68847, #7619, .T. ) ;
#28275=ADVANCED_FACE ( 'NONE', ( #128022 ), #94632, .F. ) ;
#28276=DIRECTION ( 'NONE',  ( 0.6830127018922181881, 0.6830127018922202975, -0.2588190451025214056 ) ) ;
#28277=VERTEX_POINT ( 'NONE', #40304 ) ;
#28278=LINE ( 'NONE', #49344, #118197 ) ;
#28280=EDGE_LOOP ( 'NONE', ( #104922, #111019, #132005, #45244 ) ) ;
#28282=CARTESIAN_POINT ( 'NONE',  ( -5.510786437626906675, -27.52281430457051314, 5.000000000000000000 ) ) ;
#28283=DIRECTION ( 'NONE',  ( 0.7071067811865486830, -0.7071067811865464625, -0.000000000000000000 ) ) ;
#28284=VERTEX_POINT ( 'NONE', #107659 ) ;
#28285=CARTESIAN_POINT ( 'NONE',  ( -8.671830600776409881, 17.25929247661554911, 4.000000000000000000 ) ) ;
#28287=ORIENTED_EDGE ( 'NONE', *, *, #98516, .F. ) ;
#28289=ORIENTED_EDGE ( 'NONE', *, *, #111727, .F. ) ;
#28291=ORIENTED_EDGE ( 'NONE', *, *, #89180, .T. ) ;
#28292=CARTESIAN_POINT ( 'NONE',  ( -31.49999999999977973, 6.052185695429109558, 5.000000000000000000 ) ) ;
#28293=DIRECTION ( 'NONE',  ( -0.3543493200069162685, -0.000000000000000000, -0.9351131265310288487 ) ) ;
#28294=LINE ( 'NONE', #105813, #84496 ) ;
#28295=ADVANCED_FACE ( 'NONE', ( #17097 ), #50447, .F. ) ;
#28296=CARTESIAN_POINT ( 'NONE',  ( -33.69326993309579166, -3.740707523384244837, 12.88036043432875388 ) ) ;
#28298=VECTOR ( 'NONE', #98229, 999.9999999999998863 ) ;
#28299=VECTOR ( 'NONE', #128976, 999.9999999999998863 ) ;
#28300=LINE ( 'NONE', #52867, #16846 ) ;
#28301=ADVANCED_FACE ( 'NONE', ( #106207 ), #8317, .F. ) ;
#28302=VECTOR ( 'NONE', #124408, 1000.000000000000000 ) ;
#28305=PLANE ( 'NONE',  #129338 ) ;
#28306=CARTESIAN_POINT ( 'NONE',  ( -34.47516574401892342, -11.97193265888405200, 4.998110765256834398 ) ) ;
#28308=VERTEX_POINT ( 'NONE', #117794 ) ;
#28309=ORIENTED_EDGE ( 'NONE', *, *, #103114, .T. ) ;
#28310=VECTOR ( 'NONE', #30154, 1000.000000000000000 ) ;
#28311=EDGE_LOOP ( 'NONE', ( #130483, #74611, #131634, #54374 ) ) ;
#28312=VECTOR ( 'NONE', #32860, 1000.000000000000000 ) ;
#28313=VERTEX_POINT ( 'NONE', #39580 ) ;
#28314=VECTOR ( 'NONE', #140230, 1000.000000000000000 ) ;
#28316=VERTEX_POINT ( 'NONE', #83816 ) ;
#28317=EDGE_CURVE ( 'NONE', #98487, #27213, #18482, .T. ) ;
#28318=VERTEX_POINT ( 'NONE', #17774 ) ;
#28321=EDGE_CURVE ( 'NONE', #48577, #35756, #62051, .T. ) ;
#28322=EDGE_CURVE ( 'NONE', #43125, #26437, #118537, .T. ) ;
#28323=DIRECTION ( 'NONE',  ( 0.000000000000000000, -1.000000000000000000, 0.000000000000000000 ) ) ;
#28324=ORIENTED_EDGE ( 'NONE', *, *, #73067, .T. ) ;
#28325=DIRECTION ( 'NONE',  ( -0.000000000000000000, -0.3543493200069152693, 0.9351131265310292928 ) ) ;
#28327=CARTESIAN_POINT ( 'NONE',  ( 34.75611968250419181, 20.81293425470717651, 4.955485411084878500 ) ) ;
#28330=ORIENTED_EDGE ( 'NONE', *, *, #63803, .T. ) ;
#28333=EDGE_CURVE ( 'NONE', #24066, #59015, #27236, .T. ) ;
#28334=PLANE ( 'NONE',  #113656 ) ;
#28335=ORIENTED_EDGE ( 'NONE', *, *, #100798, .F. ) ;
#28336=EDGE_LOOP ( 'NONE', ( #16042, #86527, #66773 ) ) ;
#28337=SURFACE_STYLE_FILL_AREA ( #113900 ) ;
#28338=ORIENTED_EDGE ( 'NONE', *, *, #131964, .F. ) ;
#28339=LINE ( 'NONE', #30473, #129794 ) ;
#28340=EDGE_CURVE ( 'NONE', #132946, #488, #67033, .T. ) ;
#28341=CYLINDRICAL_SURFACE ( 'NONE', #70525, 0.5000000000000004441 ) ;
#28342=ORIENTED_EDGE ( 'NONE', *, *, #93125, .T. ) ;
#28343=VECTOR ( 'NONE', #125829, 1000.000000000000000 ) ;
#28345=AXIS2_PLACEMENT_3D ( 'NONE', #78788, #11332, #12074 ) ;
#28346=CARTESIAN_POINT ( 'NONE',  ( -34.42500000000001137, 14.97718569542927014, 5.000000000000000000 ) ) ;
#28347=DIRECTION ( 'NONE',  ( 0.7071067811865486830, -0.7071067811865464625, -0.000000000000000000 ) ) ;
#28348=VERTEX_POINT ( 'NONE', #55445 ) ;
#28349=CARTESIAN_POINT ( 'NONE',  ( -2.999999999999981792, 7.588810512006209485, -3.013526669885219889 ) ) ;
#28351=DIRECTION ( 'NONE',  ( 0.7071067811865487940, 0.7071067811865463515, 0.000000000000000000 ) ) ;
#28352=ORIENTED_EDGE ( 'NONE', *, *, #139445, .T. ) ;
#28353=PLANE ( 'NONE',  #57944 ) ;
#28354=ORIENTED_EDGE ( 'NONE', *, *, #71521, .T. ) ;
#28355=ORIENTED_EDGE ( 'NONE', *, *, #57916, .F. ) ;
#28356=CARTESIAN_POINT ( 'NONE',  ( -11.99999999999992006, 14.58746187583910192, 4.000000000000000000 ) ) ;
#28358=EDGE_LOOP ( 'NONE', ( #97553, #84936, #78559, #94393 ) ) ;
#28360=ADVANCED_FACE ( 'NONE', ( #20645 ), #111217, .F. ) ;
#28361=FACE_OUTER_BOUND ( 'NONE', #58845, .T. ) ;
#28362=ADVANCED_FACE ( 'NONE', ( #108339 ), #88797, .F. ) ;
#28363=CARTESIAN_POINT ( 'NONE',  ( -34.45011844616454511, 18.00230414159377190, 5.000000000000000888 ) ) ;
#28364=ORIENTED_EDGE ( 'NONE', *, *, #37969, .F. ) ;
#28367=CARTESIAN_POINT ( 'NONE',  ( 68.99451991528748351, 28.92564299267986172, 4.000000000000000000 ) ) ;
#28368=CARTESIAN_POINT ( 'NONE',  ( 24.29974487139158867, -27.71228299555223273, 4.000000000000000000 ) ) ;
#28369=AXIS2_PLACEMENT_3D ( 'NONE', #30013, #85824, #74254 ) ;
#28370=CARTESIAN_POINT ( 'NONE',  ( 26.99999999999981526, -0.03360074219773204196, 5.000000000000000000 ) ) ;
#28371=CARTESIAN_POINT ( 'NONE',  ( -57.48921356237308800, -27.52281430457095368, 5.000000000000000000 ) ) ;
#28372=VECTOR ( 'NONE', #31598, 1000.000000000000000 ) ;
#28373=FACE_OUTER_BOUND ( 'NONE', #35882, .T. ) ;
#28376=PLANE ( 'NONE',  #59327 ) ;
#28377=ORIENTED_EDGE ( 'NONE', *, *, #11876, .F. ) ;
#28378=ORIENTED_EDGE ( 'NONE', *, *, #64111, .T. ) ;
#28381=ORIENTED_EDGE ( 'NONE', *, *, #10425, .T. ) ;
#28382=EDGE_LOOP ( 'NONE', ( #117678, #141279 ) ) ;
#28383=VERTEX_POINT ( 'NONE', #130155 ) ;
#28384=CARTESIAN_POINT ( 'NONE',  ( -48.48921356237309510, -27.52281430457089328, 5.000000000000000000 ) ) ;
#28386=ORIENTED_EDGE ( 'NONE', *, *, #72395, .F. ) ;
#28389=DIRECTION ( 'NONE',  ( -0.6830127018922180770, -0.6830127018922204085, -0.2588190451025213501 ) ) ;
#28390=CARTESIAN_POINT ( 'NONE',  ( 31.49999999999977263, 16.18958161055405043, -11.56426086740804138 ) ) ;
#28394=LINE ( 'NONE', #17495, #5299 ) ;
#28396=VECTOR ( 'NONE', #13033, 999.9999999999998863 ) ;
#28400=CARTESIAN_POINT ( 'NONE',  ( -27.09843580608220392, 11.25929247661560950, 10.79108189686400721 ) ) ;
#28401=DIRECTION ( 'NONE',  ( -0.3543493200069162685, -0.000000000000000000, -0.9351131265310288487 ) ) ;
#28402=ORIENTED_EDGE ( 'NONE', *, *, #69563, .F. ) ;
#28403=VERTEX_POINT ( 'NONE', #44606 ) ;
#28405=VERTEX_POINT ( 'NONE', #98918 ) ;
#28406=CARTESIAN_POINT ( 'NONE',  ( -54.18398860626899705, 28.73617430169825226, 5.000000000000000000 ) ) ;
#28407=EDGE_CURVE ( 'NONE', #118585, #131755, #32262, .T. ) ;
#28408=PLANE ( 'NONE',  #15402 ) ;
#28409=VECTOR ( 'NONE', #127094, 999.9999999999998863 ) ;
#28410=VECTOR ( 'NONE', #125970, 999.9999999999998863 ) ;
#28411=DIRECTION ( 'NONE',  ( 0.7071067811865487940, -0.7071067811865463515, 0.000000000000000000 ) ) ;
#28413=AXIS2_PLACEMENT_3D ( 'NONE', #137440, #27953, #38131 ) ;
#28415=DIRECTION ( 'NONE',  ( -0.7071067811865487940, 0.7071067811865463515, 0.000000000000000000 ) ) ;
#28416=VECTOR ( 'NONE', #60412, 1000.000000000000000 ) ;
#28419=CARTESIAN_POINT ( 'NONE',  ( 6.299744871391586898, -27.71228299555210484, 4.000000000000000000 ) ) ;
#28420=VERTEX_POINT ( 'NONE', #64900 ) ;
#28421=VECTOR ( 'NONE', #82801, 1000.000000000000000 ) ;
#28422=CARTESIAN_POINT ( 'NONE',  ( -6.838293875473762107, -6.740707523384212863, 16.75550250614865888 ) ) ;
#28423=CARTESIAN_POINT ( 'NONE',  ( 30.48921356237309510, -27.52281430457076894, 5.000000000000000000 ) ) ;
#28424=LINE ( 'NONE', #84931, #109231 ) ;
#28425=ADVANCED_FACE ( 'NONE', ( #121390 ), #102355, .F. ) ;
#28427=ORIENTED_EDGE ( 'NONE', *, *, #61087, .F. ) ;
#28430=EDGE_CURVE ( 'NONE', #29863, #33461, #131573, .T. ) ;
#28431=ORIENTED_EDGE ( 'NONE', *, *, #9655, .F. ) ;
#28432=DIRECTION ( 'NONE',  ( 1.000000000000000000, 0.000000000000000000, 0.000000000000000000 ) ) ;
#28433=FACE_OUTER_BOUND ( 'NONE', #105766, .T. ) ;
#28437=ADVANCED_FACE ( 'NONE', ( #9014 ), #42448, .F. ) ;
#28438=VECTOR ( 'NONE', #69194, 1000.000000000000000 ) ;
#28440=VERTEX_POINT ( 'NONE', #43146 ) ;
#28441=DIRECTION ( 'NONE',  ( 1.000000000000000000, 0.000000000000000000, 0.000000000000000000 ) ) ;
#28442=EDGE_CURVE ( 'NONE', #117951, #54976, #21384, .T. ) ;
#28443=LINE ( 'NONE', #63239, #31653 ) ;
#28444=ORIENTED_EDGE ( 'NONE', *, *, #125315, .T. ) ;
#28446=LINE ( 'NONE', #59659, #33158 ) ;
#28447=EDGE_LOOP ( 'NONE', ( #63912, #69037, #141231, #43824 ) ) ;
#28448=VECTOR ( 'NONE', #108658, 1000.000000000000000 ) ;
#28449=EDGE_CURVE ( 'NONE', #100336, #66493, #143150, .T. ) ;
#28452=EDGE_LOOP ( 'NONE', ( #1640, #15920, #89965, #43301 ) ) ;
#28453=VECTOR ( 'NONE', #67025, 1000.000000000000000 ) ;
#28454=CARTESIAN_POINT ( 'NONE',  ( 34.58990935480147755, 9.759292476615625489, 11.28811694763786733 ) ) ;
#28455=VECTOR ( 'NONE', #6064, 1000.000000000000000 ) ;
#28456=VECTOR ( 'NONE', #96135, 1000.000000000000000 ) ;
#28457=EDGE_CURVE ( 'NONE', #13719, #110313, #94295, .T. ) ;
#28458=DIRECTION ( 'NONE',  ( -0.7071067811865486830, -0.7071067811865464625, 0.000000000000000000 ) ) ;
#28459=FACE_BOUND ( 'NONE', #97100, .T. ) ;
#28460=CARTESIAN_POINT ( 'NONE',  ( 34.92499999999998295, 22.22500000000000142, 4.500000000000000888 ) ) ;
#28461=PLANE ( 'NONE',  #34079 ) ;
#28462=ORIENTED_EDGE ( 'NONE', *, *, #24503, .T. ) ;
#28463=DIRECTION ( 'NONE',  ( 0.6830127018922180770, -0.6830127018922204085, -0.2588190451025213501 ) ) ;
#28464=DIRECTION ( 'NONE',  ( 0.7071067811865486830, -0.7071067811865464625, -0.000000000000000000 ) ) ;
#28465=EDGE_LOOP ( 'NONE', ( #55166, #1548, #59594, #62242 ) ) ;
#28466=EDGE_CURVE ( 'NONE', #100977, #32778, #113916, .T. ) ;
#28468=CARTESIAN_POINT ( 'NONE',  ( -20.56494995367816614, -2.598550695876024275, 5.000000000000000000 ) ) ;
#28469=ORIENTED_EDGE ( 'NONE', *, *, #71350, .F. ) ;
#28470=VECTOR ( 'NONE', #97122, 1000.000000000000000 ) ;
#28471=VERTEX_POINT ( 'NONE', #103044 ) ;
#28473=ORIENTED_EDGE ( 'NONE', *, *, #128991, .F. ) ;
#28474=FACE_OUTER_BOUND ( 'NONE', #92525, .T. ) ;
#28475=PLANE ( 'NONE',  #47389 ) ;
#28476=VECTOR ( 'NONE', #4463, 1000.000000000000114 ) ;
#28477=ADVANCED_FACE ( 'NONE', ( #116765 ), #4366, .F. ) ;
#28478=ORIENTED_EDGE ( 'NONE', *, *, #49256, .F. ) ;
#28479=CARTESIAN_POINT ( 'NONE',  ( -24.48921356237309510, -27.52281430457072631, 5.000000000000000000 ) ) ;
#28481=ADVANCED_FACE ( 'NONE', ( #137830 ), #70468, .F. ) ;
#28482=PLANE ( 'NONE',  #114973 ) ;
#28483=PLANE ( 'NONE',  #43605 ) ;
#28485=ADVANCED_FACE ( 'NONE', ( #116039 ), #48669, .T. ) ;
#28486=LINE ( 'NONE', #27031, #79473 ) ;
#28488=ORIENTED_EDGE ( 'NONE', *, *, #41132, .F. ) ;
#28489=VECTOR ( 'NONE', #62136, 1000.000000000000000 ) ;
#28490=ORIENTED_EDGE ( 'NONE', *, *, #24228, .T. ) ;
#28492=DIRECTION ( 'NONE',  ( -0.6830127018922180770, -0.6830127018922204085, -0.2588190451025213501 ) ) ;
#28493=ORIENTED_EDGE ( 'NONE', *, *, #95539, .F. ) ;
#28494=ADVANCED_FACE ( 'NONE', ( #115294 ), #3685, .T. ) ;
#28495=VERTEX_POINT ( 'NONE', #124790 ) ;
#28496=VERTEX_POINT ( 'NONE', #25461 ) ;
#28497=CARTESIAN_POINT ( 'NONE',  ( 36.29974487139159578, -27.71228299555231445, 4.000000000000000000 ) ) ;
#28498=AXIS2_PLACEMENT_3D ( 'NONE', #7127, #51409, #139858 ) ;
#28499=EDGE_LOOP ( 'NONE', ( #109879, #62542, #103760, #12047 ) ) ;
#28506=EDGE_CURVE ( 'NONE', #46033, #66739, #61018, .T. ) ;
#28507=CARTESIAN_POINT ( 'NONE',  ( -13.00193056682089043, -22.22500000000000142, 4.500000000000000888 ) ) ;
#28508=DIRECTION ( 'NONE',  ( 0.7071067811865486830, -0.7071067811865464625, -0.000000000000000000 ) ) ;
#28509=VECTOR ( 'NONE', #77578, 999.9999999999998863 ) ;
#28510=CARTESIAN_POINT ( 'NONE',  ( -13.49999999999990763, 11.52377502935402198, -1.522421517564052751 ) ) ;
#28511=ORIENTED_EDGE ( 'NONE', *, *, #2100, .F. ) ;
#28512=DIRECTION ( 'NONE',  ( 0.7071067811865487940, 0.7071067811865463515, 0.000000000000000000 ) ) ;
#28513=ORIENTED_EDGE ( 'NONE', *, *, #1401, .F. ) ;
#28514=DIRECTION ( 'NONE',  ( 0.7071067811865487940, 0.7071067811865463515, 0.000000000000000000 ) ) ;
#28515=EDGE_CURVE ( 'NONE', #66659, #73980, #38505, .T. ) ;
#28516=CARTESIAN_POINT ( 'NONE',  ( -18.48921356237309510, -27.52281430457068367, 5.000000000000000000 ) ) ;
#28517=AXIS2_PLACEMENT_3D ( 'NONE', #1539, #122632, #23303 ) ;
#28518=LINE ( 'NONE', #5291, #44836 ) ;
#28520=ORIENTED_EDGE ( 'NONE', *, *, #68849, .F. ) ;
#28521=DIRECTION ( 'NONE',  ( 0.6830127018922181881, 0.6830127018922202975, -0.2588190451025214056 ) ) ;
#28522=CARTESIAN_POINT ( 'NONE',  ( -14.51078643762690490, -27.52281430457045275, 5.000000000000000000 ) ) ;
#28523=DIRECTION ( 'NONE',  ( -0.6830127018922181881, 0.6830127018922202975, -0.2588190451025214056 ) ) ;
#28524=AXIS2_PLACEMENT_3D ( 'NONE', #132763, #20369, #107397 ) ;
#28526=CARTESIAN_POINT ( 'NONE',  ( 6.060110710440158144, -9.740707523384187994, 10.89222023123379302 ) ) ;
#28527=CARTESIAN_POINT ( 'NONE',  ( 27.18398860626900060, 28.73617430169806042, 5.000000000000000000 ) ) ;
#28529=DIRECTION ( 'NONE',  ( -0.6830127018922181881, 0.6830127018922202975, -0.2588190451025214056 ) ) ;
#28530=CARTESIAN_POINT ( 'NONE',  ( 10.82816939922345867, 9.759292476615614831, 4.000000000000000000 ) ) ;
#28531=VERTEX_POINT ( 'NONE', #82044 ) ;
#28532=EDGE_CURVE ( 'NONE', #49419, #1370, #69734, .T. ) ;
#28534=LINE ( 'NONE', #83644, #68025 ) ;
#28535=DIRECTION ( 'NONE',  ( -0.6830127018922181881, 0.6830127018922202975, -0.2588190451025214056 ) ) ;
#28537=LINE ( 'NONE', #39414, #138464 ) ;
#28538=AXIS2_PLACEMENT_3D ( 'NONE', #29936, #106053, #130723 ) ;
#28539=DIRECTION ( 'NONE',  ( -0.000000000000000000, 0.000000000000000000, 1.000000000000000000 ) ) ;
#28540=CARTESIAN_POINT ( 'NONE',  ( -32.48334561358932149, 22.22500000000000142, 4.500000000000000888 ) ) ;
#28541=CARTESIAN_POINT ( 'NONE',  ( 16.49999999999988276, 14.14708470758592540, -0.5283514160166939977 ) ) ;
#28542=ORIENTED_EDGE ( 'NONE', *, *, #120572, .F. ) ;
#28543=DIRECTION ( 'NONE',  ( 0.6830127018922181881, 0.6830127018922202975, -0.2588190451025214056 ) ) ;
#28544=CARTESIAN_POINT ( 'NONE',  ( 3.459838389497381872, 18.75929247661552779, 8.305906642995493527 ) ) ;
#28546=CARTESIAN_POINT ( 'NONE',  ( -0.7071067811865398012, -3.740707523384244837, 5.000000000000000000 ) ) ;
#28548=EDGE_CURVE ( 'NONE', #142104, #20334, #37808, .T. ) ;
#28549=VECTOR ( 'NONE', #85169, 1000.000000000000227 ) ;
#28552=ORIENTED_EDGE ( 'NONE', *, *, #29628, .T. ) ;
#28553=CARTESIAN_POINT ( 'NONE',  ( 12.45512140948705415, 22.22500000000000142, 22.95409916400075900 ) ) ;
#28554=ORIENTED_EDGE ( 'NONE', *, *, #49754, .T. ) ;
#28555=VERTEX_POINT ( 'NONE', #15988 ) ;
#28556=CARTESIAN_POINT ( 'NONE',  ( 11.51078643762690490, -27.52281430457047406, 5.000000000000000000 ) ) ;
#28557=PLANE ( 'NONE',  #106238 ) ;
#28558=DIRECTION ( 'NONE',  ( -0.7071067811865487940, 0.7071067811865463515, -0.000000000000000000 ) ) ;
#28559=VECTOR ( 'NONE', #51156, 1000.000000000000000 ) ;
#28560=CARTESIAN_POINT ( 'NONE',  ( -2.293876922608026003, 22.22500000000000142, 4.000000000000000000 ) ) ;
#28561=EDGE_CURVE ( 'NONE', #13220, #141911, #60277, .T. ) ;
#28562=LINE ( 'NONE', #26415, #44131 ) ;
#28564=EDGE_LOOP ( 'NONE', ( #114187, #105495, #87074, #58858 ) ) ;
#28565=LINE ( 'NONE', #63360, #127708 ) ;
#28566=CARTESIAN_POINT ( 'NONE',  ( -24.18398860626899705, 28.73617430169804265, 5.000000000000000000 ) ) ;
#28569=FACE_OUTER_BOUND ( 'NONE', #20487, .T. ) ;
#28570=DIRECTION ( 'NONE',  ( -0.3543493200069163240, -0.000000000000000000, 0.9351131265310288487 ) ) ;
#28571=AXIS2_PLACEMENT_3D ( 'NONE', #41821, #143266, #54167 ) ;
#28573=VECTOR ( 'NONE', #62053, 1000.000000000000000 ) ;
#28574=DIRECTION ( 'NONE',  ( -0.7071067811865486830, 0.7071067811865464625, 0.000000000000000000 ) ) ;
#28575=ORIENTED_EDGE ( 'NONE', *, *, #63637, .F. ) ;
#28576=VERTEX_POINT ( 'NONE', #5113 ) ;
#28577=( BOUNDED_CURVE ( )  B_SPLINE_CURVE ( 3, ( #113984, #126289, #14675, #26968 ),
 .UNSPECIFIED., .F., .T. ) 
 B_SPLINE_CURVE_WITH_KNOTS ( ( 4, 4 ),
 ( 1.964434688349484315, 3.503810798801450854 ),
 .UNSPECIFIED. ) 
 CURVE ( )  GEOMETRIC_REPRESENTATION_ITEM ( )  RATIONAL_B_SPLINE_CURVE ( ( 1.000000000000000000, 0.8120851936182275077, 0.8120851936182275077, 1.000000000000000000 ) ) 
 REPRESENTATION_ITEM ( '' )  );
#28579=PLANE ( 'NONE',  #63273 ) ;
#28580=DIRECTION ( 'NONE',  ( -1.000000000000000000, 0.000000000000000000, 0.000000000000000000 ) ) ;
#28581=AXIS2_PLACEMENT_3D ( 'NONE', #49101, #60713, #81743 ) ;
#28583=ORIENTED_EDGE ( 'NONE', *, *, #80030, .T. ) ;
#28584=DIRECTION ( 'NONE',  ( 2.781805975412905274E-17, -0.3543493200069152138, 0.9351131265310292928 ) ) ;
#28585=CARTESIAN_POINT ( 'NONE',  ( 1.110173228882102237, -22.22499999999999787, 4.785647885939354751 ) ) ;
#28587=ORIENTED_EDGE ( 'NONE', *, *, #99810, .T. ) ;
#28588=ADVANCED_FACE ( 'NONE', ( #49413 ), #82729, .F. ) ;
#28589=FACE_OUTER_BOUND ( 'NONE', #22383, .T. ) ;
#28590=VERTEX_POINT ( 'NONE', #5833 ) ;
#28591=VERTEX_POINT ( 'NONE', #83443 ) ;
#28592=VECTOR ( 'NONE', #79217, 1000.000000000000000 ) ;
#28593=CARTESIAN_POINT ( 'NONE',  ( 12.70710678118645198, 20.25929247661551003, 5.000000000000000000 ) ) ;
#28595=LINE ( 'NONE', #81565, #39725 ) ;
#28596=PLANE ( 'NONE',  #90311 ) ;
#28597=FACE_OUTER_BOUND ( 'NONE', #76200, .T. ) ;
#28598=EDGE_CURVE ( 'NONE', #39505, #129536, #61704, .T. ) ;
#28599=ADVANCED_FACE ( 'NONE', ( #36368 ), #80596, .F. ) ;
#28601=ORIENTED_EDGE ( 'NONE', *, *, #67581, .T. ) ;
#28602=LINE ( 'NONE', #72857, #92377 ) ;
#28603=LINE ( 'NONE', #42344, #89394 ) ;
#28604=VECTOR ( 'NONE', #117014, 1000.000000000000000 ) ;
#28605=PLANE ( 'NONE',  #19274 ) ;
#28607=CARTESIAN_POINT ( 'NONE',  ( -29.99999999999978328, 17.96639925780208102, 5.000000000000000000 ) ) ;
#28609=EDGE_LOOP ( 'NONE', ( #1499, #97149, #126990, #85272 ) ) ;
#28610=EDGE_CURVE ( 'NONE', #71524, #89805, #129065, .T. ) ;
#28612=VECTOR ( 'NONE', #81820, 999.9999999999998863 ) ;
#28614=DIRECTION ( 'NONE',  ( -0.7071067811865486830, 0.7071067811865464625, 0.000000000000000000 ) ) ;
#28615=DIRECTION ( 'NONE',  ( -0.3543493200069162685, -0.000000000000000000, -0.9351131265310288487 ) ) ;
#28616=CARTESIAN_POINT ( 'NONE',  ( -34.92500000000001137, -22.22500000000000142, 4.500000000000000888 ) ) ;
#28617=EDGE_CURVE ( 'NONE', #20377, #45045, #95728, .T. ) ;
#28618=CARTESIAN_POINT ( 'NONE',  ( -21.32816939922337696, 14.25929247661557753, 4.000000000000000000 ) ) ;
#28620=ORIENTED_EDGE ( 'NONE', *, *, #86927, .F. ) ;
#28621=ORIENTED_EDGE ( 'NONE', *, *, #110411, .F. ) ;
#28622=EDGE_CURVE ( 'NONE', #14566, #3084, #41334, .T. ) ;
#28623=FACE_OUTER_BOUND ( 'NONE', #38888, .T. ) ;
#28624=DIRECTION ( 'NONE',  ( 0.7071067811865486830, -0.7071067811865464625, -0.000000000000000000 ) ) ;
#28625=EDGE_LOOP ( 'NONE', ( #35645, #70866, #93255, #60037 ) ) ;
#28627=ADVANCED_FACE ( 'NONE', ( #108001 ), #84856, .T. ) ;
#28628=ORIENTED_EDGE ( 'NONE', *, *, #136515, .T. ) ;
#28629=CARTESIAN_POINT ( 'NONE',  ( -21.48921356237309155, -27.52281430457070499, 5.000000000000000000 ) ) ;
#28630=VERTEX_POINT ( 'NONE', #108709 ) ;
#28632=CARTESIAN_POINT ( 'NONE',  ( 34.92499999999998295, 4.701930566820937685, 4.500000000000000888 ) ) ;
#28634=ADVANCED_FACE ( 'NONE', ( #7261 ), #96410, .F. ) ;
#28635=FACE_BOUND ( 'NONE', #92468, .T. ) ;
#28636=DIRECTION ( 'NONE',  ( -0.7071067811865486830, -0.7071067811865464625, 0.000000000000000000 ) ) ;
#28637=DIRECTION ( 'NONE',  ( 0.3543493200069162685, -0.000000000000000000, -0.9351131265310288487 ) ) ;
#28638=DIRECTION ( 'NONE',  ( 0.7071067811865487940, 0.7071067811865463515, -0.000000000000000000 ) ) ;
#28639=ORIENTED_EDGE ( 'NONE', *, *, #138710, .T. ) ;
#28641=EDGE_CURVE ( 'NONE', #47477, #28496, #118164, .T. ) ;
#28645=EDGE_LOOP ( 'NONE', ( #55699, #54321, #24173, #100740 ) ) ;
#28649=PLANE ( 'NONE',  #386 ) ;
#28650=VECTOR ( 'NONE', #56719, 1000.000000000000000 ) ;
#28651=LINE ( 'NONE', #72903, #10898 ) ;
#28652=CARTESIAN_POINT ( 'NONE',  ( -20.99999999999984013, 11.58746187583912324, 4.000000000000000000 ) ) ;
#28655=CARTESIAN_POINT ( 'NONE',  ( -34.92500000000001137, 22.22500000000000142, 4.000000000000000000 ) ) ;
#28656=FACE_OUTER_BOUND ( 'NONE', #117804, .T. ) ;
#28658=PLANE ( 'NONE',  #78194 ) ;
#28659=FACE_OUTER_BOUND ( 'NONE', #4251, .T. ) ;
#28660=EDGE_CURVE ( 'NONE', #13520, #70281, #85549, .T. ) ;
#28661=DIRECTION ( 'NONE',  ( 0.6830127018922181881, 0.6830127018922202975, -0.2588190451025214056 ) ) ;
#28663=DIRECTION ( 'NONE',  ( -0.7071067811865486830, 0.7071067811865464625, 0.000000000000000000 ) ) ;
#28664=EDGE_LOOP ( 'NONE', ( #8712, #92068, #68677, #61736, #69215, #71369 ) ) ;
#28665=CARTESIAN_POINT ( 'NONE',  ( 0.000000000000000000, 10.21212019023809425, -2.019456568337797187 ) ) ;
#28666=ADVANCED_FACE ( 'NONE', ( #30486 ), #74725, .F. ) ;
#28668=VECTOR ( 'NONE', #103904, 1000.000000000000000 ) ;
#28669=ORIENTED_EDGE ( 'NONE', *, *, #91681, .F. ) ;
#28673=ORIENTED_EDGE ( 'NONE', *, *, #3987, .T. ) ;
#28674=AXIS2_PLACEMENT_3D ( 'NONE', #53619, #31159, #42757 ) ;
#28679=EDGE_CURVE ( 'NONE', #43879, #111424, #118901, .T. ) ;
#28680=DIRECTION ( 'NONE',  ( 0.7071067811865486830, -0.7071067811865464625, -0.000000000000000000 ) ) ;
#28681=VERTEX_POINT ( 'NONE', #18128 ) ;
#28682=SPHERICAL_SURFACE ( 'NONE', #113564, 0.5000000000000000000 ) ;
#28683=AXIS2_PLACEMENT_3D ( 'NONE', #133221, #136045, #112174 ) ;
#28686=ORIENTED_EDGE ( 'NONE', *, *, #87190, .F. ) ;
#28687=VERTEX_POINT ( 'NONE', #128376 ) ;
#28688=CARTESIAN_POINT ( 'NONE',  ( -45.48921356237309510, -27.52281430457087197, 5.000000000000000000 ) ) ;
#28691=CARTESIAN_POINT ( 'NONE',  ( -35.99451991528749772, 28.92564299267963079, 4.000000000000000000 ) ) ;
#28692=ORIENTED_EDGE ( 'NONE', *, *, #71997, .F. ) ;
#28695=ORIENTED_EDGE ( 'NONE', *, *, #53166, .T. ) ;
#28696=ORIENTED_EDGE ( 'NONE', *, *, #31879, .F. ) ;
#28697=CARTESIAN_POINT ( 'NONE',  ( 0.000000000000000000, -7.068876922607745250, 4.000000000000000000 ) ) ;
#28698=VECTOR ( 'NONE', #61188, 1000.000000000000227 ) ;
#28700=DIRECTION ( 'NONE',  ( 0.7071067811865487940, 0.7071067811865463515, 0.000000000000000000 ) ) ;
#28702=CARTESIAN_POINT ( 'NONE',  ( -29.67183060077626422, -21.74070752338406010, 4.000000000000000000 ) ) ;
#28703=ORIENTED_EDGE ( 'NONE', *, *, #63637, .T. ) ;
#28704=LINE ( 'NONE', #96061, #79012 ) ;
#28705=VERTEX_POINT ( 'NONE', #62411 ) ;
#28706=CARTESIAN_POINT ( 'NONE',  ( 57.48921356237308800, -27.52281430457095368, 5.000000000000000000 ) ) ;
#28708=EDGE_CURVE ( 'NONE', #12409, #47805, #31204, .T. ) ;
#28709=CARTESIAN_POINT ( 'NONE',  ( 0.000000000000000000, 0.000000000000000000, 5.000000000000000000 ) ) ;
#28710=VECTOR ( 'NONE', #140123, 999.9999999999998863 ) ;
#28711=CARTESIAN_POINT ( 'NONE',  ( 2.187538124160505415, -22.22500000000000142, 4.000000000000000000 ) ) ;
#28713=ORIENTED_EDGE ( 'NONE', *, *, #38592, .T. ) ;
#28714=EDGE_LOOP ( 'NONE', ( #13135, #73655, #120558, #85999 ) ) ;
#28715=EDGE_LOOP ( 'NONE', ( #129696, #42268, #61373, #39847 ) ) ;
#28716=CARTESIAN_POINT ( 'NONE',  ( 0.000000000000000000, 0.000000000000000000, 5.000000000000000000 ) ) ;
#28717=CARTESIAN_POINT ( 'NONE',  ( -18.48921356237309510, -27.52281430457068367, 5.000000000000000000 ) ) ;
#28719=CARTESIAN_POINT ( 'NONE',  ( -34.49999999999974420, -17.94567065516885762, 4.994342998332165884 ) ) ;
#28722=VECTOR ( 'NONE', #27351, 1000.000000000000000 ) ;
#28725=DIRECTION ( 'NONE',  ( -0.7071067811865486830, -0.7071067811865464625, -0.000000000000000000 ) ) ;
#28726=EDGE_CURVE ( 'NONE', #38372, #15838, #41670, .T. ) ;
#28727=DIRECTION ( 'NONE',  ( -0.7071067811865486830, -0.7071067811865464625, -0.000000000000000000 ) ) ;
#28729=CARTESIAN_POINT ( 'NONE',  ( 5.510786437626906675, -27.52281430457051314, 5.000000000000000000 ) ) ;
#28732=VERTEX_POINT ( 'NONE', #21746 ) ;
#28733=CARTESIAN_POINT ( 'NONE',  ( 45.48921356237309510, -27.52281430457087197, 5.000000000000000000 ) ) ;
#28734=CARTESIAN_POINT ( 'NONE',  ( 34.45011844616452379, -16.48371918836233618, 5.000000000000000888 ) ) ;
#28735=EDGE_LOOP ( 'NONE', ( #124249, #103039, #6293, #18726 ) ) ;
#28736=ADVANCED_FACE ( 'NONE', ( #10832 ), #89839, .F. ) ;
#28740=ORIENTED_EDGE ( 'NONE', *, *, #90259, .T. ) ;
#28741=FACE_OUTER_BOUND ( 'NONE', #62863, .T. ) ;
#28742=FACE_OUTER_BOUND ( 'NONE', #108997, .T. ) ;
#28743=VECTOR ( 'NONE', #30055, 1000.000000000000000 ) ;
#28744=DIRECTION ( 'NONE',  ( -0.7071067811865487940, 0.7071067811865463515, -0.000000000000000000 ) ) ;
#28746=FACE_OUTER_BOUND ( 'NONE', #87234, .T. ) ;
#28747=VECTOR ( 'NONE', #59258, 1000.000000000000227 ) ;
#28749=ORIENTED_EDGE ( 'NONE', *, *, #84087, .F. ) ;
#28753=CARTESIAN_POINT ( 'NONE',  ( -20.51078643762690490, -27.52281430457041012, 5.000000000000000000 ) ) ;
#28754=ORIENTED_EDGE ( 'NONE', *, *, #83233, .T. ) ;
#28755=CARTESIAN_POINT ( 'NONE',  ( -18.18398860626898994, 28.73617430169800002, 5.000000000000000000 ) ) ;
#28756=ORIENTED_EDGE ( 'NONE', *, *, #48574, .T. ) ;
#28758=DIRECTION ( 'NONE',  ( 0.7071067811865486830, -0.7071067811865464625, -0.000000000000000000 ) ) ;
#28759=EDGE_CURVE ( 'NONE', #65937, #25994, #46649, .T. ) ;
#28760=CARTESIAN_POINT ( 'NONE',  ( 32.99451991528749062, 28.92564299267960948, 4.000000000000000000 ) ) ;
#28762=EDGE_LOOP ( 'NONE', ( #81984, #16445, #80653, #37772 ) ) ;
#28763=CARTESIAN_POINT ( 'NONE',  ( -24.70710678118636494, -6.740707523384212863, 5.000000000000000000 ) ) ;
#28764=VECTOR ( 'NONE', #98061, 1000.000000000000227 ) ;
#28765=LINE ( 'NONE', #62110, #37216 ) ;
#28766=AXIS2_PLACEMENT_3D ( 'NONE', #105163, #137817, #5099 ) ;
#28767=FACE_OUTER_BOUND ( 'NONE', #8254, .T. ) ;
#28768=EDGE_CURVE ( 'NONE', #125118, #135031, #45670, .T. ) ;
#28769=CARTESIAN_POINT ( 'NONE',  ( 69.48921356237309510, -27.52281430457103895, 5.000000000000000000 ) ) ;
#28770=ORIENTED_EDGE ( 'NONE', *, *, #120357, .T. ) ;
#28771=PLANE ( 'NONE',  #57667 ) ;
#28772=CARTESIAN_POINT ( 'NONE',  ( -31.49999999999977973, 3.653845994658361906, -4.504631822206299319 ) ) ;
#28774=CARTESIAN_POINT ( 'NONE',  ( -30.51168605928413058, 6.759292476615653023, 16.35960578974476576 ) ) ;
#28776=ORIENTED_EDGE ( 'NONE', *, *, #32006, .F. ) ;
#28777=ORIENTED_EDGE ( 'NONE', *, *, #25610, .F. ) ;
#28778=ADVANCED_FACE ( 'NONE', ( #54404 ), #87710, .F. ) ;
#28780=AXIS2_PLACEMENT_3D ( 'NONE', #29907, #10296, #75584 ) ;
#28781=VERTEX_POINT ( 'NONE', #66686 ) ;
#28783=DIRECTION ( 'NONE',  ( -0.7071067811865486830, -0.7071067811865464625, 0.000000000000000000 ) ) ;
#28785=CARTESIAN_POINT ( 'NONE',  ( 6.812461875839422198, -22.22500000000000142, 4.000000000000000000 ) ) ;
#28786=CARTESIAN_POINT ( 'NONE',  ( 9.005480084712511157, 28.92564299267931816, 4.000000000000000000 ) ) ;
#28787=ORIENTED_EDGE ( 'NONE', *, *, #116467, .T. ) ;
#28789=CARTESIAN_POINT ( 'NONE',  ( -32.99999999999975842, 11.58746187583912146, 4.000000000000000000 ) ) ;
#28791=ORIENTED_EDGE ( 'NONE', *, *, #54417, .F. ) ;
#28792=ADVANCED_FACE ( 'NONE', ( #100027 ), #683, .F. ) ;
#28793=FACE_OUTER_BOUND ( 'NONE', #8283, .T. ) ;
#28794=CARTESIAN_POINT ( 'NONE',  ( -0.1839886062690032631, 28.73617430169787568, 5.000000000000000000 ) ) ;
#28796=LINE ( 'NONE', #49846, #81696 ) ;
#28797=ORIENTED_EDGE ( 'NONE', *, *, #82655, .T. ) ;
#28798=ORIENTED_EDGE ( 'NONE', *, *, #112598, .F. ) ;
#28799=EDGE_CURVE ( 'NONE', #41413, #43020, #111607, .T. ) ;
#28800=EDGE_CURVE ( 'NONE', #83105, #68726, #98579, .T. ) ;
#28801=LINE ( 'NONE', #115040, #10677 ) ;
#28802=PLANE ( 'NONE',  #113351 ) ;
#28803=CARTESIAN_POINT ( 'NONE',  ( -53.99451991528749062, 28.92564299267975869, 4.000000000000000000 ) ) ;
#28805=LINE ( 'NONE', #17875, #96682 ) ;
#28808=VERTEX_POINT ( 'NONE', #43495 ) ;
#28809=VERTEX_POINT ( 'NONE', #56568 ) ;
#28810=EDGE_LOOP ( 'NONE', ( #83247, #102508, #117543, #104415 ) ) ;
#28811=ORIENTED_EDGE ( 'NONE', *, *, #78528, .F. ) ;
#28812=VECTOR ( 'NONE', #74474, 999.9999999999998863 ) ;
#28814=DIRECTION ( 'NONE',  ( 1.000000000000000000, 0.000000000000000000, 0.000000000000000000 ) ) ;
#28815=VERTEX_POINT ( 'NONE', #79011 ) ;
#28816=DIRECTION ( 'NONE',  ( -0.000000000000000000, 0.000000000000000000, 1.000000000000000000 ) ) ;
#28817=LINE ( 'NONE', #15728, #20188 ) ;
#28820=CARTESIAN_POINT ( 'NONE',  ( 57.18398860626899705, 28.73617430169827358, 5.000000000000000000 ) ) ;
#28822=CARTESIAN_POINT ( 'NONE',  ( -5.966809772938240997, -22.22500000000000142, -5.973340791029712271 ) ) ;
#28824=ORIENTED_EDGE ( 'NONE', *, *, #19905, .T. ) ;
#28825=DIRECTION ( 'NONE',  ( -0.000000000000000000, -0.3543493200069152693, 0.9351131265310292928 ) ) ;
#28826=VERTEX_POINT ( 'NONE', #19352 ) ;
#28829=ORIENTED_EDGE ( 'NONE', *, *, #89372, .T. ) ;
#28831=VECTOR ( 'NONE', #1514, 999.9999999999998863 ) ;
#28832=EDGE_LOOP ( 'NONE', ( #75953, #35115, #48001, #10900 ) ) ;
#28833=EDGE_CURVE ( 'NONE', #69258, #92363, #72210, .T. ) ;
#28834=VECTOR ( 'NONE', #81367, 1000.000000000000000 ) ;
#28835=DIRECTION ( 'NONE',  ( -0.7071067811865486830, -0.7071067811865464625, 0.000000000000000000 ) ) ;
#28837=FACE_OUTER_BOUND ( 'NONE', #24432, .T. ) ;
#28838=AXIS2_PLACEMENT_3D ( 'NONE', #70668, #102568, #71357 ) ;
#28839=EDGE_CURVE ( 'NONE', #92154, #105072, #43265, .T. ) ;
#28840=DIRECTION ( 'NONE',  ( -0.7071067811865486830, -0.7071067811865464625, -0.000000000000000000 ) ) ;
#28841=DIRECTION ( 'NONE',  ( -0.7071067811865486830, 0.7071067811865464625, 0.000000000000000000 ) ) ;
#28843=( BOUNDED_CURVE ( )  B_SPLINE_CURVE ( 3, ( #117383, #4294, #51461, #81245 ),
 .UNSPECIFIED., .F., .F. ) 
 B_SPLINE_CURVE_WITH_KNOTS ( ( 4, 4 ),
 ( 5.106027341939290309, 6.645403452391242638 ),
 .UNSPECIFIED. ) 
 CURVE ( )  GEOMETRIC_REPRESENTATION_ITEM ( )  RATIONAL_B_SPLINE_CURVE ( ( 1.000000000000000000, 0.8120851936182307274, 0.8120851936182307274, 1.000000000000000000 ) ) 
 REPRESENTATION_ITEM ( '' )  );
#28845=VERTEX_POINT ( 'NONE', #73725 ) ;
#28846=VECTOR ( 'NONE', #124436, 1000.000000000000000 ) ;
#28847=LINE ( 'NONE', #50595, #19746 ) ;
#28848=EDGE_CURVE ( 'NONE', #130662, #53059, #117906, .T. ) ;
#28849=ORIENTED_EDGE ( 'NONE', *, *, #64145, .F. ) ;
#28850=EDGE_LOOP ( 'NONE', ( #94622, #3550, #42579, #96495 ) ) ;
#28851=CARTESIAN_POINT ( 'NONE',  ( -2.999999999999988898, 17.58746187583907172, 4.000000000000000000 ) ) ;
#28852=VERTEX_POINT ( 'NONE', #95176 ) ;
#28853=( BOUNDED_CURVE ( )  B_SPLINE_CURVE ( 3, ( #112290, #2040, #123888, #68799 ),
 .UNSPECIFIED., .F., .T. ) 
 B_SPLINE_CURVE_WITH_KNOTS ( ( 4, 4 ),
 ( 2.001653308786171426, 3.503810798801451742 ),
 .UNSPECIFIED. ) 
 CURVE ( )  GEOMETRIC_REPRESENTATION_ITEM ( )  RATIONAL_B_SPLINE_CURVE ( ( 1.000000000000000000, 0.8206354192515243895, 0.8206354192515243895, 1.000000000000000000 ) ) 
 REPRESENTATION_ITEM ( '' )  );
#28854=CARTESIAN_POINT ( 'NONE',  ( 26.87852683662837094, -20.24070752338407075, 7.412974875817730513 ) ) ;
#28855=PLANE ( 'NONE',  #22331 ) ;
#28856=EDGE_CURVE ( 'NONE', #63590, #101471, #125695, .T. ) ;
#28858=CARTESIAN_POINT ( 'NONE',  ( -0.4892135623730947680, -27.52281430457055578, 5.000000000000000000 ) ) ;
#28859=EDGE_LOOP ( 'NONE', ( #99613, #77583, #14371, #85451 ) ) ;
#28861=VERTEX_POINT ( 'NONE', #50270 ) ;
#28862=VECTOR ( 'NONE', #135325, 1000.000000000000227 ) ;
#28865=CARTESIAN_POINT ( 'NONE',  ( -10.63753812416090483, 22.22500000000000142, 4.000000000000000000 ) ) ;
#28866=VECTOR ( 'NONE', #2073, 1000.000000000000000 ) ;
#28867=FACE_OUTER_BOUND ( 'NONE', #122319, .T. ) ;
#28870=ORIENTED_EDGE ( 'NONE', *, *, #20089, .F. ) ;
#28871=ORIENTED_EDGE ( 'NONE', *, *, #134198, .F. ) ;
#28872=ORIENTED_EDGE ( 'NONE', *, *, #87073, .F. ) ;
#28873=LINE ( 'NONE', #139797, #62618 ) ;
#28875=DIRECTION ( 'NONE',  ( -0.000000000000000000, -0.3543493200069152693, 0.9351131265310292928 ) ) ;
#28876=FACE_OUTER_BOUND ( 'NONE', #41630, .T. ) ;
#28877=DIRECTION ( 'NONE',  ( 0.7071067811865487940, 0.7071067811865463515, 0.000000000000000000 ) ) ;
#28878=DIRECTION ( 'NONE',  ( -0.7071067811865487940, -0.7071067811865463515, -0.000000000000000000 ) ) ;
#28879=CARTESIAN_POINT ( 'NONE',  ( 35.99451991528749772, 28.92564299267963079, 4.000000000000000000 ) ) ;
#28880=EDGE_CURVE ( 'NONE', #127352, #46830, #48848, .T. ) ;
#28881=DIRECTION ( 'NONE',  ( -0.7071067811865486830, -0.7071067811865464625, -0.000000000000000000 ) ) ;
#28883=ORIENTED_EDGE ( 'NONE', *, *, #51149, .T. ) ;
#28885=FACE_OUTER_BOUND ( 'NONE', #140812, .T. ) ;
#28886=ORIENTED_EDGE ( 'NONE', *, *, #85433, .F. ) ;
#28887=DIRECTION ( 'NONE',  ( -0.7071067811865486830, 0.7071067811865464625, 0.000000000000000000 ) ) ;
#28888=EDGE_CURVE ( 'NONE', #105446, #135400, #93048, .T. ) ;
#28889=FACE_OUTER_BOUND ( 'NONE', #15199, .T. ) ;
#28890=EDGE_LOOP ( 'NONE', ( #37027, #45275, #111744, #133617 ) ) ;
#28891=EDGE_CURVE ( 'NONE', #91471, #4002, #72052, .T. ) ;
#28892=CARTESIAN_POINT ( 'NONE',  ( -17.99999999999986855, 13.55218569542903140, 5.000000000000000000 ) ) ;
#28894=EDGE_LOOP ( 'NONE', ( #52789, #105573, #41649, #63845 ) ) ;
#28895=DIRECTION ( 'NONE',  ( -0.7071067811865486830, -0.7071067811865464625, -0.000000000000000000 ) ) ;
#28897=ORIENTED_EDGE ( 'NONE', *, *, #66392, .F. ) ;
#28900=PLANE ( 'NONE',  #23011 ) ;
#28901=CARTESIAN_POINT ( 'NONE',  ( 57.18398860626899705, 28.73617430169827358, 5.000000000000000000 ) ) ;
#28903=DIRECTION ( 'NONE',  ( -0.6830127018922181881, 0.6830127018922202975, -0.2588190451025214056 ) ) ;
#28904=CARTESIAN_POINT ( 'NONE',  ( 20.99999999999985079, -6.033600742197678279, 5.000000000000000000 ) ) ;
#28908=CARTESIAN_POINT ( 'NONE',  ( 6.328169399223488867, -12.74070752338414891, 4.000000000000000000 ) ) ;
#28909=LINE ( 'NONE', #39814, #84847 ) ;
#28910=ORIENTED_EDGE ( 'NONE', *, *, #75838, .T. ) ;
#28911=ADVANCED_FACE ( 'NONE', ( #50979 ), #105340, .F. ) ;
#28912=AXIS2_PLACEMENT_3D ( 'NONE', #98532, #142758, #42035 ) ;
#28913=ORIENTED_EDGE ( 'NONE', *, *, #40905, .T. ) ;
#28916=ORIENTED_EDGE ( 'NONE', *, *, #11523, .F. ) ;
#28918=CARTESIAN_POINT ( 'NONE',  ( -51.18398860626899705, 28.73617430169823095, 5.000000000000000000 ) ) ;
#28919=ORIENTED_EDGE ( 'NONE', *, *, #77214, .T. ) ;
#28920=CARTESIAN_POINT ( 'NONE',  ( -23.03457404400602115, 22.22500000000000142, 0.4942731178105737033 ) ) ;
#28921=FACE_OUTER_BOUND ( 'NONE', #53055, .T. ) ;
#28924=FACE_OUTER_BOUND ( 'NONE', #44545, .T. ) ;
#28925=DIRECTION ( 'NONE',  ( -0.000000000000000000, 0.3543493200069153248, 0.9351131265310292928 ) ) ;
#28927=DIRECTION ( 'NONE',  ( 0.7071067811865487940, -0.7071067811865463515, 0.000000000000000000 ) ) ;
#28928=DIRECTION ( 'NONE',  ( 0.6830127018922181881, 0.6830127018922202975, -0.2588190451025214056 ) ) ;
#28929=CARTESIAN_POINT ( 'NONE',  ( -72.48921356237309510, -27.52281430457106026, 5.000000000000000000 ) ) ;
#28930=DIRECTION ( 'NONE',  ( -0.7071067811865486830, -0.7071067811865464625, -0.000000000000000000 ) ) ;
#28931=DIRECTION ( 'NONE',  ( -0.000000000000000000, 0.3543493200069153248, 0.9351131265310292928 ) ) ;
#28932=ADVANCED_FACE ( 'NONE', ( #61872 ), #103199, .F. ) ;
#28933=VECTOR ( 'NONE', #23763, 1000.000000000000000 ) ;
#28935=ORIENTED_EDGE ( 'NONE', *, *, #137551, .T. ) ;
#28936=ADVANCED_FACE ( 'NONE', ( #61190 ), #40133, .F. ) ;
#28938=ORIENTED_EDGE ( 'NONE', *, *, #25508, .T. ) ;
#28939=ADVANCED_FACE ( 'NONE', ( #82208 ), #116228, .T. ) ;
#28940=VECTOR ( 'NONE', #82446, 1000.000000000000000 ) ;
#28941=DIRECTION ( 'NONE',  ( -0.7071067811865487940, 0.7071067811865463515, 0.000000000000000000 ) ) ;
#28943=ORIENTED_EDGE ( 'NONE', *, *, #111896, .T. ) ;
#28944=ADVANCED_FACE ( 'NONE', ( #15442 ), #115469, .F. ) ;
#28945=ADVANCED_FACE ( 'NONE', ( #114084 ), #38673, .F. ) ;
#28946=CARTESIAN_POINT ( 'NONE',  ( -16.78678096696630817, 12.75929247661558996, 10.29404684609031406 ) ) ;
#28949=VECTOR ( 'NONE', #138368, 1000.000000000000000 ) ;
#28950=ORIENTED_EDGE ( 'NONE', *, *, #29725, .F. ) ;
#28951=DIRECTION ( 'NONE',  ( -0.3543493200069162685, -0.000000000000000000, -0.9351131265310288487 ) ) ;
#28952=ORIENTED_EDGE ( 'NONE', *, *, #127623, .T. ) ;
#28953=LINE ( 'NONE', #18762, #66199 ) ;
#28955=FACE_OUTER_BOUND ( 'NONE', #6408, .T. ) ;
#28956=ORIENTED_EDGE ( 'NONE', *, *, #14225, .T. ) ;
#28957=VERTEX_POINT ( 'NONE', #27785 ) ;
#28958=EDGE_CURVE ( 'NONE', #132946, #18156, #59048, .T. ) ;
#28959=VERTEX_POINT ( 'NONE', #71313 ) ;
#28960=PLANE ( 'NONE',  #2820 ) ;
#28961=EDGE_CURVE ( 'NONE', #63922, #17176, #3846, .T. ) ;
#28962=DIRECTION ( 'NONE',  ( 0.7071067811865487940, 0.7071067811865463515, -0.000000000000000000 ) ) ;
#28964=CARTESIAN_POINT ( 'NONE',  ( 0.000000000000000000, 0.000000000000000000, 5.000000000000000000 ) ) ;
#28965=EDGE_CURVE ( 'NONE', #36826, #96824, #92311, .T. ) ;
#28967=AXIS2_PLACEMENT_3D ( 'NONE', #88775, #45987, #22739 ) ;
#28969=ORIENTED_EDGE ( 'NONE', *, *, #475, .F. ) ;
#28970=VECTOR ( 'NONE', #83226, 1000.000000000000000 ) ;
#28971=ORIENTED_EDGE ( 'NONE', *, *, #116301, .T. ) ;
#28972=CARTESIAN_POINT ( 'NONE',  ( -16.49999999999988276, -16.53360074219757792, 5.000000000000000000 ) ) ;
#28974=ORIENTED_EDGE ( 'NONE', *, *, #38437, .F. ) ;
#28975=ADVANCED_FACE ( 'NONE', ( #16159 ), #72781, .F. ) ;
#28978=CARTESIAN_POINT ( 'NONE',  ( 27.70710678118635428, 20.25929247661551003, 5.000000000000000000 ) ) ;
#28979=ORIENTED_EDGE ( 'NONE', *, *, #81092, .T. ) ;
#28981=DIRECTION ( 'NONE',  ( 0.7071067811865487940, 0.7071067811865463515, -0.000000000000000000 ) ) ;
#28982=ADVANCED_FACE ( 'NONE', ( #137991 ), #82903, .T. ) ;
#28983=FACE_OUTER_BOUND ( 'NONE', #102915, .T. ) ;
#28985=ORIENTED_EDGE ( 'NONE', *, *, #45474, .T. ) ;
#28986=CARTESIAN_POINT ( 'NONE',  ( -24.87485380690750958, -14.24070752338413470, 9.401115078912718914 ) ) ;
#28987=DIRECTION ( 'NONE',  ( -0.6830127018922180770, -0.6830127018922204085, -0.2588190451025213501 ) ) ;
#28988=EDGE_LOOP ( 'NONE', ( #95949, #27343, #59455, #103944 ) ) ;
#28989=DIRECTION ( 'NONE',  ( -0.7071067811865487940, 0.7071067811865463515, -0.000000000000000000 ) ) ;
#28990=DIRECTION ( 'NONE',  ( -0.000000000000000000, 0.000000000000000000, 1.000000000000000000 ) ) ;
#28992=EDGE_LOOP ( 'NONE', ( #140431, #65810, #50911, #116049 ) ) ;
#28994=CARTESIAN_POINT ( 'NONE',  ( -6.005480084712508493, 28.92564299267933947, 4.000000000000000000 ) ) ;
#28995=VERTEX_POINT ( 'NONE', #140811 ) ;
#28996=ORIENTED_EDGE ( 'NONE', *, *, #68249, .F. ) ;
#28997=VERTEX_POINT ( 'NONE', #131393 ) ;
#28998=EDGE_CURVE ( 'NONE', #59037, #122865, #64708, .T. ) ;
#29002=LINE ( 'NONE', #140598, #93540 ) ;
#29004=CARTESIAN_POINT ( 'NONE',  ( 3.469446951953614189E-15, -10.44781430457072169, 5.000000000000000000 ) ) ;
#29005=CARTESIAN_POINT ( 'NONE',  ( -15.32816939922342137, -18.74070752338409562, 4.000000000000000000 ) ) ;
#29006=CARTESIAN_POINT ( 'NONE',  ( 33.48921356237309510, -27.52281430457078670, 5.000000000000000000 ) ) ;
#29007=CARTESIAN_POINT ( 'NONE',  ( -11.99451991528749417, 28.92564299267946382, 4.000000000000000000 ) ) ;
#29008=CARTESIAN_POINT ( 'NONE',  ( 21.75860074219781382, 21.72500000000000142, 5.000000000000000000 ) ) ;
#29009=CARTESIAN_POINT ( 'NONE',  ( -66.18398860626901126, 28.73617430169833753, 5.000000000000000000 ) ) ;
#29010=PLANE ( 'NONE',  #742 ) ;
#29011=EDGE_CURVE ( 'NONE', #39017, #86313, #22176, .T. ) ;
#29012=EDGE_LOOP ( 'NONE', ( #37244, #13283, #85090, #13761 ) ) ;
#29013=ORIENTED_EDGE ( 'NONE', *, *, #143542, .F. ) ;
#29014=VERTEX_POINT ( 'NONE', #119069 ) ;
#29015=ORIENTED_EDGE ( 'NONE', *, *, #126649, .F. ) ;
#29017=ORIENTED_EDGE ( 'NONE', *, *, #44256, .T. ) ;
#29018=ORIENTED_EDGE ( 'NONE', *, *, #56853, .F. ) ;
#29020=CARTESIAN_POINT ( 'NONE',  ( 6.489213562373093325, -27.52281430457059841, 5.000000000000000000 ) ) ;
#29022=DIRECTION ( 'NONE',  ( 0.7071067811865487940, -0.7071067811865463515, 0.000000000000000000 ) ) ;
#29023=ORIENTED_EDGE ( 'NONE', *, *, #86749, .F. ) ;
#29024=FACE_OUTER_BOUND ( 'NONE', #130903, .T. ) ;
#29025=ORIENTED_EDGE ( 'NONE', *, *, #58671, .F. ) ;
#29027=CARTESIAN_POINT ( 'NONE',  ( -33.48921356237309510, -27.52281430457078670, 5.000000000000000000 ) ) ;
#29029=LINE ( 'NONE', #63814, #82094 ) ;
#29035=CARTESIAN_POINT ( 'NONE',  ( -20.99451991528748707, 28.92564299267952777, 4.000000000000000000 ) ) ;
#29036=ORIENTED_EDGE ( 'NONE', *, *, #25073, .T. ) ;
#29037=VERTEX_POINT ( 'NONE', #73451 ) ;
#29039=ORIENTED_EDGE ( 'NONE', *, *, #51281, .F. ) ;
#29041=LINE ( 'NONE', #74713, #90484 ) ;
#29043=DIRECTION ( 'NONE',  ( -0.000000000000000000, -0.3543493200069152693, 0.9351131265310292928 ) ) ;
#29044=ORIENTED_EDGE ( 'NONE', *, *, #116994, .F. ) ;
#29045=LINE ( 'NONE', #70463, #82958 ) ;
#29046=VECTOR ( 'NONE', #113575, 999.9999999999998863 ) ;
#29047=EDGE_CURVE ( 'NONE', #132587, #24646, #108165, .T. ) ;
#29048=LINE ( 'NONE', #51531, #9537 ) ;
#29049=DIRECTION ( 'NONE',  ( -0.3543493200069162685, -0.000000000000000000, -0.9351131265310288487 ) ) ;
#29050=ORIENTED_EDGE ( 'NONE', *, *, #127103, .T. ) ;
#29052=LINE ( 'NONE', #94296, #128071 ) ;
#29053=ORIENTED_EDGE ( 'NONE', *, *, #118928, .T. ) ;
#29054=EDGE_CURVE ( 'NONE', #2836, #94406, #119761, .T. ) ;
#29056=ORIENTED_EDGE ( 'NONE', *, *, #131077, .F. ) ;
#29057=ADVANCED_FACE ( 'NONE', ( #87165 ), #10302, .F. ) ;
#29058=VERTEX_POINT ( 'NONE', #29915 ) ;
#29059=DIRECTION ( 'NONE',  ( -0.3543493200069162685, -0.000000000000000000, -0.9351131265310288487 ) ) ;
#29060=DIRECTION ( 'NONE',  ( -0.7071067811865487940, 0.7071067811865463515, 0.000000000000000000 ) ) ;
#29062=CARTESIAN_POINT ( 'NONE',  ( 29.99999999999979750, 4.552185695429124657, 5.000000000000000000 ) ) ;
#29063=AXIS2_PLACEMENT_3D ( 'NONE', #139857, #15856, #28927 ) ;
#29064=DIRECTION ( 'NONE',  ( 0.7071067811865486830, -0.7071067811865464625, -0.000000000000000000 ) ) ;
#29065=AXIS2_PLACEMENT_3D ( 'NONE', #79799, #134141, #58788 ) ;
#29066=LINE ( 'NONE', #37823, #41452 ) ;
#29067=AXIS2_PLACEMENT_3D ( 'NONE', #117941, #7769, #129558 ) ;
#29068=EDGE_CURVE ( 'NONE', #18156, #133583, #62022, .T. ) ;
#29069=LINE ( 'NONE', #62428, #39225 ) ;
#29070=DIRECTION ( 'NONE',  ( 0.6830127018922181881, 0.6830127018922202975, -0.2588190451025214056 ) ) ;
#29071=DIRECTION ( 'NONE',  ( 0.7071067811865486830, -0.7071067811865464625, -0.000000000000000000 ) ) ;
#29072=LINE ( 'NONE', #95015, #132766 ) ;
#29073=LINE ( 'NONE', #85572, #51215 ) ;
#29074=CARTESIAN_POINT ( 'NONE',  ( -35.99451991528749772, 28.92564299267963079, 4.000000000000000000 ) ) ;
#29075=LINE ( 'NONE', #18153, #39117 ) ;
#29077=DIRECTION ( 'NONE',  ( -0.7071067811865486830, -0.7071067811865464625, -0.000000000000000000 ) ) ;
#29078=LINE ( 'NONE', #63169, #15268 ) ;
#29079=ORIENTED_EDGE ( 'NONE', *, *, #17404, .T. ) ;
#29081=ORIENTED_EDGE ( 'NONE', *, *, #37812, .F. ) ;
#29084=ORIENTED_EDGE ( 'NONE', *, *, #24015, .T. ) ;
#29085=ORIENTED_EDGE ( 'NONE', *, *, #63832, .T. ) ;
#29086=EDGE_LOOP ( 'NONE', ( #48411, #142742, #1845, #112967 ) ) ;
#29087=DIRECTION ( 'NONE',  ( -0.7071067811865486830, -0.7071067811865464625, 0.000000000000000000 ) ) ;
#29088=PLANE ( 'NONE',  #120284 ) ;
#29089=VERTEX_POINT ( 'NONE', #120462 ) ;
#29090=CARTESIAN_POINT ( 'NONE',  ( -20.99451991528748707, 28.92564299267952777, 4.000000000000000000 ) ) ;
#29092=CARTESIAN_POINT ( 'NONE',  ( -26.51078643762690845, -27.52281430457036748, 5.000000000000000000 ) ) ;
#29096=DIRECTION ( 'NONE',  ( 0.6830127018922181881, 0.6830127018922202975, -0.2588190451025214056 ) ) ;
#29098=FACE_OUTER_BOUND ( 'NONE', #137865, .T. ) ;
#29099=DIRECTION ( 'NONE',  ( -0.6830127018922180770, -0.6830127018922204085, -0.2588190451025213501 ) ) ;
#29100=LINE ( 'NONE', #126967, #67743 ) ;
#29101=LINE ( 'NONE', #83502, #45449 ) ;
#29103=DIRECTION ( 'NONE',  ( -0.7071067811865486830, -0.7071067811865464625, 0.000000000000000000 ) ) ;
#29104=DIRECTION ( 'NONE',  ( -0.7071067811865486830, 0.7071067811865464625, 0.000000000000000000 ) ) ;
#29105=VERTEX_POINT ( 'NONE', #85722 ) ;
#29106=ORIENTED_EDGE ( 'NONE', *, *, #87858, .T. ) ;
#29110=FACE_OUTER_BOUND ( 'NONE', #42224, .T. ) ;
#29112=DIRECTION ( 'NONE',  ( -0.7071067811865487940, 0.7071067811865463515, 0.000000000000000000 ) ) ;
#29114=EDGE_CURVE ( 'NONE', #74762, #36287, #53850, .T. ) ;
#29115=EDGE_CURVE ( 'NONE', #76368, #119902, #108881, .T. ) ;
#29118=ORIENTED_EDGE ( 'NONE', *, *, #3650, .F. ) ;
#29119=DIRECTION ( 'NONE',  ( -0.6830127018922181881, 0.6830127018922202975, -0.2588190451025214056 ) ) ;
#29120=ORIENTED_EDGE ( 'NONE', *, *, #53699, .F. ) ;
#29121=CARTESIAN_POINT ( 'NONE',  ( 6.489213562373093325, -27.52281430457059841, 5.000000000000000000 ) ) ;
#29122=ADVANCED_FACE ( 'NONE', ( #18302 ), #11712, .F. ) ;
#29123=LINE ( 'NONE', #4439, #24502 ) ;
#29124=FACE_OUTER_BOUND ( 'NONE', #54895, .T. ) ;
#29125=VERTEX_POINT ( 'NONE', #46573 ) ;
#29127=EDGE_CURVE ( 'NONE', #2713, #36832, #21902, .T. ) ;
#29129=FACE_OUTER_BOUND ( 'NONE', #100487, .T. ) ;
#29130=EDGE_CURVE ( 'NONE', #84298, #99644, #134253, .T. ) ;
#29134=AXIS2_PLACEMENT_3D ( 'NONE', #14503, #36961, #115921 ) ;
#29135=EDGE_CURVE ( 'NONE', #10533, #49354, #13857, .T. ) ;
#29136=ADVANCED_FACE ( 'NONE', ( #90762 ), #55262, .F. ) ;
#29138=ORIENTED_EDGE ( 'NONE', *, *, #1616, .F. ) ;
#29139=VECTOR ( 'NONE', #79287, 1000.000000000000000 ) ;
#29142=EDGE_LOOP ( 'NONE', ( #18223, #129781, #58495, #9357 ) ) ;
#29143=ORIENTED_EDGE ( 'NONE', *, *, #48732, .F. ) ;
#29144=ADVANCED_FACE ( 'NONE', ( #34221 ), #58154, .F. ) ;
#29145=ORIENTED_EDGE ( 'NONE', *, *, #12462, .T. ) ;
#29147=VERTEX_POINT ( 'NONE', #35688 ) ;
#29149=ADVANCED_FACE ( 'NONE', ( #111026 ), #24760, .F. ) ;
#29150=LINE ( 'NONE', #72718, #122926 ) ;
#29151=FACE_BOUND ( 'NONE', #9802, .T. ) ;
#29153=EDGE_LOOP ( 'NONE', ( #83382, #22458, #141075, #139896, #84020 ) ) ;
#29157=EDGE_LOOP ( 'NONE', ( #102316, #12140, #1136, #138097 ) ) ;
#29158=LINE ( 'NONE', #85668, #98063 ) ;
#29160=EDGE_LOOP ( 'NONE', ( #57089, #51356, #33410, #108398 ) ) ;
#29161=ADVANCED_FACE ( 'NONE', ( #3001 ), #121908, .F. ) ;
#29162=VECTOR ( 'NONE', #112727, 1000.000000000000000 ) ;
#29164=VERTEX_POINT ( 'NONE', #45134 ) ;
#29165=VECTOR ( 'NONE', #117447, 1000.000000000000000 ) ;
#29166=PLANE ( 'NONE',  #25535 ) ;
#29168=CARTESIAN_POINT ( 'NONE',  ( 47.99451991528749062, 28.92564299267971251, 4.000000000000000000 ) ) ;
#29169=VERTEX_POINT ( 'NONE', #79912 ) ;
#29170=FACE_OUTER_BOUND ( 'NONE', #53316, .T. ) ;
#29171=VECTOR ( 'NONE', #100055, 1000.000000000000000 ) ;
#29172=EDGE_CURVE ( 'NONE', #74481, #127430, #89312, .T. ) ;
#29173=CARTESIAN_POINT ( 'NONE',  ( 0.000000000000000000, 2.342191155542447500, -5.001666872980086609 ) ) ;
#29175=CARTESIAN_POINT ( 'NONE',  ( 6.183988606268994381, 28.73617430169791476, 5.000000000000000000 ) ) ;
#29176=PLANE ( 'NONE',  #69420 ) ;
#29177=VERTEX_POINT ( 'NONE', #123397 ) ;
#29178=ORIENTED_EDGE ( 'NONE', *, *, #92806, .F. ) ;
#29179=CARTESIAN_POINT ( 'NONE',  ( -26.67183060077628198, -18.74070752338408852, 4.000000000000000000 ) ) ;
#29182=ORIENTED_EDGE ( 'NONE', *, *, #107976, .F. ) ;
#29183=ORIENTED_EDGE ( 'NONE', *, *, #129141, .T. ) ;
#29184=DIRECTION ( 'NONE',  ( -0.6830127018922181881, 0.6830127018922202975, -0.2588190451025214056 ) ) ;
#29186=LINE ( 'NONE', #106728, #16058 ) ;
#29187=ORIENTED_EDGE ( 'NONE', *, *, #24514, .T. ) ;
#29189=CARTESIAN_POINT ( 'NONE',  ( -66.29974487139159578, -27.71228299555252406, 4.000000000000000000 ) ) ;
#29191=FACE_OUTER_BOUND ( 'NONE', #11822, .T. ) ;
#29192=ORIENTED_EDGE ( 'NONE', *, *, #28961, .T. ) ;
#29194=LINE ( 'NONE', #95161, #109120 ) ;
#29195=EDGE_CURVE ( 'NONE', #23129, #54018, #45830, .T. ) ;
#29196=DIRECTION ( 'NONE',  ( 0.6830127018922181881, 0.6830127018922202975, -0.2588190451025214056 ) ) ;
#29197=DIRECTION ( 'NONE',  ( -0.000000000000000000, -0.3543493200069152693, 0.9351131265310292928 ) ) ;
#29198=ORIENTED_EDGE ( 'NONE', *, *, #124363, .F. ) ;
#29199=VECTOR ( 'NONE', #128079, 1000.000000000000000 ) ;
#29203=CARTESIAN_POINT ( 'NONE',  ( -34.43312800248720862, -21.74070752338405299, 6.915939825044155498 ) ) ;
#29204=CARTESIAN_POINT ( 'NONE',  ( -20.67183060077632817, 20.25929247661551003, 4.000000000000000000 ) ) ;
#29205=ORIENTED_EDGE ( 'NONE', *, *, #119689, .F. ) ;
#29206=PLANE ( 'NONE',  #142119 ) ;
#29207=PLANE ( 'NONE',  #104342 ) ;
#29209=ORIENTED_EDGE ( 'NONE', *, *, #72650, .T. ) ;
#29210=DIRECTION ( 'NONE',  ( -0.7071067811865486830, -0.7071067811865464625, 0.000000000000000000 ) ) ;
#29211=LINE ( 'NONE', #129231, #111855 ) ;
#29213=CARTESIAN_POINT ( 'NONE',  ( -23.99999999999982947, 10.21212019023806938, -2.019456568337744340 ) ) ;
#29215=EDGE_CURVE ( 'NONE', #80017, #1190, #67592, .T. ) ;
#29217=VERTEX_POINT ( 'NONE', #24059 ) ;
#29218=DIRECTION ( 'NONE',  ( -0.3543493200069162685, -0.000000000000000000, -0.9351131265310288487 ) ) ;
#29221=ADVANCED_FACE ( 'NONE', ( #1544 ), #68317, .F. ) ;
#29222=EDGE_CURVE ( 'NONE', #4021, #3523, #124085, .T. ) ;
#29225=CARTESIAN_POINT ( 'NONE',  ( 27.29974487139158512, -27.71228299555225405, 4.000000000000000000 ) ) ;
#29226=DIRECTION ( 'NONE',  ( 0.7071067811865487940, 0.7071067811865463515, 0.000000000000000000 ) ) ;
#29228=VECTOR ( 'NONE', #61457, 1000.000000000000000 ) ;
#29229=ORIENTED_EDGE ( 'NONE', *, *, #33893, .T. ) ;
#29230=EDGE_CURVE ( 'NONE', #47662, #56422, #61016, .T. ) ;
#29233=DIRECTION ( 'NONE',  ( -0.000000000000000000, 0.000000000000000000, 1.000000000000000000 ) ) ;
#29235=CARTESIAN_POINT ( 'NONE',  ( 33.29974487139158867, -27.71228299555229313, 4.000000000000000000 ) ) ;
#29236=EDGE_CURVE ( 'NONE', #91335, #35930, #49411, .T. ) ;
#29237=ORIENTED_EDGE ( 'NONE', *, *, #100509, .T. ) ;
#29238=CARTESIAN_POINT ( 'NONE',  ( -17.20710678118642178, -17.24070752338410628, 5.000000000000000000 ) ) ;
#29239=ORIENTED_EDGE ( 'NONE', *, *, #115112, .T. ) ;
#29241=ORIENTED_EDGE ( 'NONE', *, *, #1291, .T. ) ;
#29242=FACE_OUTER_BOUND ( 'NONE', #46405, .T. ) ;
#29244=CARTESIAN_POINT ( 'NONE',  ( -18.79289321881332242, -17.24070752338410628, 5.000000000000000000 ) ) ;
#29245=LINE ( 'NONE', #137319, #104454 ) ;
#29246=LINE ( 'NONE', #141597, #131972 ) ;
#29247=VECTOR ( 'NONE', #105751, 1000.000000000000000 ) ;
#29248=DIRECTION ( 'NONE',  ( -0.000000000000000000, 0.3543493200069153248, 0.9351131265310292928 ) ) ;
#29250=ORIENTED_EDGE ( 'NONE', *, *, #51672, .T. ) ;
#29251=LINE ( 'NONE', #106800, #122711 ) ;
#29252=DIRECTION ( 'NONE',  ( 0.7071067811865487940, -0.7071067811865463515, 0.000000000000000000 ) ) ;
#29253=EDGE_CURVE ( 'NONE', #84504, #75919, #113913, .T. ) ;
#29254=DIRECTION ( 'NONE',  ( -0.6830127018922181881, 0.6830127018922202975, -0.2588190451025214056 ) ) ;
#29256=CARTESIAN_POINT ( 'NONE',  ( -2.999999999999975131, 8.587461875839162317, 4.000000000000000000 ) ) ;
#29257=VECTOR ( 'NONE', #95970, 999.9999999999998863 ) ;
#29258=CARTESIAN_POINT ( 'NONE',  ( 17.99999999999986855, -16.02097659208068947, -11.96015758381212635 ) ) ;
#29259=VECTOR ( 'NONE', #10393, 1000.000000000000000 ) ;
#29262=LINE ( 'NONE', #85784, #53048 ) ;
#29264=EDGE_LOOP ( 'NONE', ( #128488, #53735, #2650, #4408 ) ) ;
#29266=DIRECTION ( 'NONE',  ( -0.7071067811865487940, 0.7071067811865463515, -0.000000000000000000 ) ) ;
#29267=CARTESIAN_POINT ( 'NONE',  ( -11.99999999999991829, 15.45873954670184425, -0.03131636524291228629 ) ) ;
#29268=EDGE_CURVE ( 'NONE', #26466, #116177, #17446, .T. ) ;
#29269=VECTOR ( 'NONE', #123791, 999.9999999999998863 ) ;
#29270=EDGE_LOOP ( 'NONE', ( #77679, #94603, #11526, #43728 ) ) ;
#29271=DIRECTION ( 'NONE',  ( 0.7071067811865487940, 0.7071067811865463515, 0.000000000000000000 ) ) ;
#29272=ADVANCED_FACE ( 'NONE', ( #50100 ), #38503, .T. ) ;
#29273=EDGE_CURVE ( 'NONE', #106882, #35724, #126903, .T. ) ;
#29275=ORIENTED_EDGE ( 'NONE', *, *, #99785, .T. ) ;
#29276=PLANE ( 'NONE',  #27093 ) ;
#29277=EDGE_LOOP ( 'NONE', ( #35352, #141861, #104013, #132838 ) ) ;
#29278=ORIENTED_EDGE ( 'NONE', *, *, #143093, .T. ) ;
#29279=CARTESIAN_POINT ( 'NONE',  ( -8.999999999999932498, -19.06887692260762890, 4.000000000000000000 ) ) ;
#29280=ADVANCED_FACE ( 'NONE', ( #26201 ), #27604, .F. ) ;
#29282=CARTESIAN_POINT ( 'NONE',  ( 16.49999999999987921, -14.56887692260766087, 4.000000000000000000 ) ) ;
#29283=FACE_OUTER_BOUND ( 'NONE', #102109, .T. ) ;
#29285=LINE ( 'NONE', #61950, #21085 ) ;
#29286=DIRECTION ( 'NONE',  ( 0.6830127018922180770, -0.6830127018922204085, -0.2588190451025213501 ) ) ;
#29287=ORIENTED_EDGE ( 'NONE', *, *, #123795, .T. ) ;
#29288=LINE ( 'NONE', #92388, #136374 ) ;
#29289=DIRECTION ( 'NONE',  ( -0.7071067811865486830, -0.7071067811865464625, 0.000000000000000000 ) ) ;
#29290=PLANE ( 'NONE',  #88834 ) ;
#29291=CARTESIAN_POINT ( 'NONE',  ( 31.17183060077626067, 6.759292476615651246, 4.000000000000000000 ) ) ;
#29292=LINE ( 'NONE', #27869, #15949 ) ;
#29293=VERTEX_POINT ( 'NONE', #70466 ) ;
#29294=ORIENTED_EDGE ( 'NONE', *, *, #115392, .T. ) ;
#29295=VECTOR ( 'NONE', #106543, 1000.000000000000000 ) ;
#29296=EDGE_CURVE ( 'NONE', #130144, #29014, #37061, .T. ) ;
#29297=DIRECTION ( 'NONE',  ( 1.000000000000000000, 0.000000000000000000, 0.000000000000000000 ) ) ;
#29299=FACE_OUTER_BOUND ( 'NONE', #18751, .T. ) ;
#29301=LINE ( 'NONE', #127184, #66424 ) ;
#29302=ORIENTED_EDGE ( 'NONE', *, *, #103890, .F. ) ;
#29303=ORIENTED_EDGE ( 'NONE', *, *, #105533, .T. ) ;
#29306=EDGE_CURVE ( 'NONE', #58487, #67480, #103042, .T. ) ;
#29307=ORIENTED_EDGE ( 'NONE', *, *, #36295, .T. ) ;
#29308=EDGE_LOOP ( 'NONE', ( #96162, #49571, #37612 ) ) ;
#29309=DIRECTION ( 'NONE',  ( -0.000000000000000000, 0.000000000000000000, 1.000000000000000000 ) ) ;
#29311=PLANE ( 'NONE',  #24808 ) ;
#29312=VECTOR ( 'NONE', #138022, 1000.000000000000227 ) ;
#29313=DIRECTION ( 'NONE',  ( 0.3543493200069162685, -0.000000000000000000, -0.9351131265310288487 ) ) ;
#29314=AXIS2_PLACEMENT_3D ( 'NONE', #63766, #52152, #19522 ) ;
#29315=FACE_BOUND ( 'NONE', #33159, .T. ) ;
#29316=CARTESIAN_POINT ( 'NONE',  ( 3.712309939660257019, -21.73547319004780576, 4.999917730833663754 ) ) ;
#29317=PLANE ( 'NONE',  #140593 ) ;
#29318=FACE_OUTER_BOUND ( 'NONE', #17177, .T. ) ;
#29322=AXIS2_PLACEMENT_3D ( 'NONE', #4497, #94419, #72742 ) ;
#29323=EDGE_LOOP ( 'NONE', ( #133820, #131552, #37666, #76725 ) ) ;
#29324=ORIENTED_EDGE ( 'NONE', *, *, #15251, .T. ) ;
#29327=VECTOR ( 'NONE', #22866, 1000.000000000000000 ) ;
#29328=FACE_OUTER_BOUND ( 'NONE', #111433, .T. ) ;
#29329=DIRECTION ( 'NONE',  ( 0.6830127018922180770, -0.6830127018922204085, -0.2588190451025213501 ) ) ;
#29330=CARTESIAN_POINT ( 'NONE',  ( 0.000000000000000000, 0.000000000000000000, 5.000000000000000000 ) ) ;
#29331=LINE ( 'NONE', #4672, #19342 ) ;
#29332=CARTESIAN_POINT ( 'NONE',  ( 0.000000000000000000, 0.000000000000000000, 5.000000000000000000 ) ) ;
#29333=VECTOR ( 'NONE', #138281, 999.9999999999998863 ) ;
#29334=CARTESIAN_POINT ( 'NONE',  ( 19.49999999999987566, 16.08746187583907883, 4.000000000000000000 ) ) ;
#29335=DIRECTION ( 'NONE',  ( -0.7071067811865486830, -0.7071067811865464625, 0.000000000000000000 ) ) ;
#29336=LINE ( 'NONE', #112963, #120999 ) ;
#29337=PLANE ( 'NONE',  #85628 ) ;
#29338=DIRECTION ( 'NONE',  ( -0.000000000000000000, -0.3543493200069152693, 0.9351131265310292928 ) ) ;
#29340=DIRECTION ( 'NONE',  ( -0.3543493200069162685, -0.000000000000000000, -0.9351131265310288487 ) ) ;
#29341=CARTESIAN_POINT ( 'NONE',  ( 26.99451991528749417, 28.92564299267956685, 4.000000000000000000 ) ) ;
#29343=VECTOR ( 'NONE', #56978, 999.9999999999998863 ) ;
#29344=EDGE_LOOP ( 'NONE', ( #49264, #113481, #81724, #34504 ) ) ;
#29347=EDGE_LOOP ( 'NONE', ( #138341, #5452, #46189, #48276 ) ) ;
#29348=AXIS2_PLACEMENT_3D ( 'NONE', #28794, #73035, #115741 ) ;
#29349=VECTOR ( 'NONE', #17836, 1000.000000000000227 ) ;
#29353=DIRECTION ( 'NONE',  ( 0.7071067811865487940, 0.7071067811865463515, 0.000000000000000000 ) ) ;
#29355=ORIENTED_EDGE ( 'NONE', *, *, #48898, .T. ) ;
#29356=DIRECTION ( 'NONE',  ( 0.6830127018922180770, -0.6830127018922204085, -0.2588190451025213501 ) ) ;
#29357=EDGE_CURVE ( 'NONE', #129322, #88587, #125520, .T. ) ;
#29358=VECTOR ( 'NONE', #52450, 1000.000000000000227 ) ;
#29360=CARTESIAN_POINT ( 'NONE',  ( 25.49999999999982236, -12.66682484999664382, -0.6294897503863351451 ) ) ;
#29361=VERTEX_POINT ( 'NONE', #105173 ) ;
#29362=ORIENTED_EDGE ( 'NONE', *, *, #125455, .F. ) ;
#29363=DIRECTION ( 'NONE',  ( 0.6830127018922180770, -0.6830127018922204085, -0.2588190451025213501 ) ) ;
#29364=ORIENTED_EDGE ( 'NONE', *, *, #89336, .T. ) ;
#29365=CARTESIAN_POINT ( 'NONE',  ( -18.48921356237309510, -27.52281430457068367, 5.000000000000000000 ) ) ;
#29366=ORIENTED_EDGE ( 'NONE', *, *, #39044, .T. ) ;
#29367=ORIENTED_EDGE ( 'NONE', *, *, #22778, .F. ) ;
#29368=ORIENTED_EDGE ( 'NONE', *, *, #123024, .F. ) ;
#29369=ORIENTED_EDGE ( 'NONE', *, *, #49478, .F. ) ;
#29370=EDGE_CURVE ( 'NONE', #40283, #34938, #114611, .T. ) ;
#29371=EDGE_CURVE ( 'NONE', #28471, #25993, #92864, .T. ) ;
#29373=DIRECTION ( 'NONE',  ( -0.000000000000000000, 0.3543493200069153248, 0.9351131265310292928 ) ) ;
#29374=PLANE ( 'NONE',  #83900 ) ;
#29375=EDGE_CURVE ( 'NONE', #925, #110223, #60275, .T. ) ;
#29376=CARTESIAN_POINT ( 'NONE',  ( 0.000000000000000000, 0.000000000000000000, 5.000000000000000000 ) ) ;
#29377=PLANE ( 'NONE',  #76080 ) ;
#29378=ADVANCED_FACE ( 'NONE', ( #91464 ), #39217, .T. ) ;
#29379=EDGE_CURVE ( 'NONE', #134283, #93966, #124788, .T. ) ;
#29380=ORIENTED_EDGE ( 'NONE', *, *, #46707, .T. ) ;
#29381=DIRECTION ( 'NONE',  ( -0.7071067811865486830, -0.7071067811865464625, 0.000000000000000000 ) ) ;
#29382=VERTEX_POINT ( 'NONE', #73286 ) ;
#29383=VECTOR ( 'NONE', #66654, 1000.000000000000000 ) ;
#29384=LINE ( 'NONE', #17778, #84158 ) ;
#29385=ADVANCED_FACE ( 'NONE', ( #97110 ), #30484, .F. ) ;
#29386=EDGE_CURVE ( 'NONE', #104249, #13451, #8667, .T. ) ;
#29387=DIRECTION ( 'NONE',  ( 0.7071067811865487940, 0.7071067811865463515, 0.000000000000000000 ) ) ;
#29388=LINE ( 'NONE', #62764, #94813 ) ;
#29389=AXIS2_PLACEMENT_3D ( 'NONE', #26370, #89470, #111959 ) ;
#29390=ORIENTED_EDGE ( 'NONE', *, *, #87813, .F. ) ;
#29392=( BOUNDED_CURVE ( )  B_SPLINE_CURVE ( 3, ( #132468, #97644, #107791, #75216 ),
 .UNSPECIFIED., .F., .T. ) 
 B_SPLINE_CURVE_WITH_KNOTS ( ( 4, 4 ),
 ( 5.005968288816728951, 5.074607125596330093 ),
 .UNSPECIFIED. ) 
 CURVE ( )  GEOMETRIC_REPRESENTATION_ITEM ( )  RATIONAL_B_SPLINE_CURVE ( ( 1.000000000000000000, 0.9996074310407765395, 0.9996074310407765395, 1.000000000000000000 ) ) 
 REPRESENTATION_ITEM ( '' )  );
#29394=VERTEX_POINT ( 'NONE', #9391 ) ;
#29395=ORIENTED_EDGE ( 'NONE', *, *, #43913, .T. ) ;
#29396=EDGE_CURVE ( 'NONE', #112859, #2047, #106572, .T. ) ;
#29397=VERTEX_POINT ( 'NONE', #107999 ) ;
#29398=CARTESIAN_POINT ( 'NONE',  ( 63.18398860626900415, 28.73617430169831621, 5.000000000000000000 ) ) ;
#29399=DIRECTION ( 'NONE',  ( -0.6830127018922181881, 0.6830127018922202975, -0.2588190451025214056 ) ) ;
#29400=DIRECTION ( 'NONE',  ( 0.3543493200069162685, -0.000000000000000000, -0.9351131265310288487 ) ) ;
#29401=AXIS2_PLACEMENT_3D ( 'NONE', #76011, #118791, #75316 ) ;
#29402=CARTESIAN_POINT ( 'NONE',  ( 12.71230993966019085, -21.73547319004782352, 4.999917730833663754 ) ) ;
#29406=EDGE_CURVE ( 'NONE', #38491, #137243, #52907, .T. ) ;
#29407=DIRECTION ( 'NONE',  ( -0.000000000000000000, 0.000000000000000000, 1.000000000000000000 ) ) ;
#29408=LINE ( 'NONE', #73643, #25657 ) ;
#29410=PLANE ( 'NONE',  #139064 ) ;
#29412=ORIENTED_EDGE ( 'NONE', *, *, #87590, .T. ) ;
#29413=CARTESIAN_POINT ( 'NONE',  ( 27.48921356237309155, -27.52281430457074762, 5.000000000000000000 ) ) ;
#29414=ORIENTED_EDGE ( 'NONE', *, *, #125989, .F. ) ;
#29416=CARTESIAN_POINT ( 'NONE',  ( -54.48921356237310221, -27.52281430457093236, 5.000000000000000000 ) ) ;
#29418=DIRECTION ( 'NONE',  ( -0.7071067811865486830, -0.7071067811865464625, 0.000000000000000000 ) ) ;
#29420=VERTEX_POINT ( 'NONE', #53673 ) ;
#29422=LINE ( 'NONE', #95399, #132046 ) ;
#29423=CARTESIAN_POINT ( 'NONE',  ( 18.29974487139159223, -27.71228299555219010, 4.000000000000000000 ) ) ;
#29425=LINE ( 'NONE', #85962, #12572 ) ;
#29427=CARTESIAN_POINT ( 'NONE',  ( 57.48921356237308800, -27.52281430457095368, 5.000000000000000000 ) ) ;
#29428=DIRECTION ( 'NONE',  ( -0.7071067811865486830, 0.7071067811865464625, -0.000000000000000000 ) ) ;
#29429=VERTEX_POINT ( 'NONE', #86301 ) ;
#29433=ADVANCED_FACE ( 'NONE', ( #97877 ), #128374, .F. ) ;
#29434=CARTESIAN_POINT ( 'NONE',  ( 32.99999999999977263, -15.03360074219758502, 5.000000000000000000 ) ) ;
#29435=VERTEX_POINT ( 'NONE', #52222 ) ;
#29436=DIRECTION ( 'NONE',  ( 1.000000000000000000, 0.000000000000000000, 0.000000000000000000 ) ) ;
#29437=ADVANCED_FACE ( 'NONE', ( #96408 ), #7982, .F. ) ;
#29438=EDGE_LOOP ( 'NONE', ( #79816, #11326, #93145, #119497 ) ) ;
#29440=EDGE_CURVE ( 'NONE', #28258, #34677, #7258, .T. ) ;
#29441=CARTESIAN_POINT ( 'NONE',  ( -66.18398860626901126, 28.73617430169833753, 5.000000000000000000 ) ) ;
#29442=PLANE ( 'NONE',  #128080 ) ;
#29443=ORIENTED_EDGE ( 'NONE', *, *, #27435, .F. ) ;
#29444=CARTESIAN_POINT ( 'NONE',  ( 0.000000000000000000, 0.000000000000000000, 5.000000000000000000 ) ) ;
#29446=EDGE_CURVE ( 'NONE', #125983, #4875, #118899, .T. ) ;
#29447=FACE_OUTER_BOUND ( 'NONE', #89601, .T. ) ;
#29449=DIRECTION ( 'NONE',  ( 0.6830127018922180770, -0.6830127018922204085, -0.2588190451025213501 ) ) ;
#29450=FACE_OUTER_BOUND ( 'NONE', #66709, .T. ) ;
#29451=ORIENTED_EDGE ( 'NONE', *, *, #54693, .F. ) ;
#29454=FACE_OUTER_BOUND ( 'NONE', #123258, .T. ) ;
#29455=EDGE_CURVE ( 'NONE', #19220, #77121, #131216, .T. ) ;
#29456=VECTOR ( 'NONE', #74265, 999.9999999999998863 ) ;
#29458=AXIS2_PLACEMENT_3D ( 'NONE', #20202, #20926, #108627 ) ;
#29460=ORIENTED_EDGE ( 'NONE', *, *, #86165, .T. ) ;
#29463=ORIENTED_EDGE ( 'NONE', *, *, #81058, .T. ) ;
#29464=ADVANCED_FACE ( 'NONE', ( #73984 ), #40651, .F. ) ;
#29465=LINE ( 'NONE', #19317, #137916 ) ;
#29467=LINE ( 'NONE', #64989, #20242 ) ;
#29468=CARTESIAN_POINT ( 'NONE',  ( 13.49999999999991473, 10.46639925780215918, 5.000000000000000000 ) ) ;
#29469=ORIENTED_EDGE ( 'NONE', *, *, #54246, .T. ) ;
#29470=PLANE ( 'NONE',  #125437 ) ;
#29471=DIRECTION ( 'NONE',  ( 0.7071067811865486830, -0.7071067811865464625, -0.000000000000000000 ) ) ;
#29472=VERTEX_POINT ( 'NONE', #19591 ) ;
#29473=FACE_OUTER_BOUND ( 'NONE', #100522, .T. ) ;
#29474=CARTESIAN_POINT ( 'NONE',  ( 29.99999999999979039, 2.966399257802232459, 5.000000000000000000 ) ) ;
#29475=CARTESIAN_POINT ( 'NONE',  ( 19.56363873141800624, -2.772201803466310288, 4.368625942145807350 ) ) ;
#29476=ORIENTED_EDGE ( 'NONE', *, *, #108014, .F. ) ;
#29477=VERTEX_POINT ( 'NONE', #120293 ) ;
#29478=ADVANCED_FACE ( 'NONE', ( #20288 ), #64527, .F. ) ;
#29479=CARTESIAN_POINT ( 'NONE',  ( 34.49999999999976552, 3.431123077392151277, 4.000000000000000000 ) ) ;
#29480=LINE ( 'NONE', #6983, #18432 ) ;
#29481=CARTESIAN_POINT ( 'NONE',  ( -21.48921356237309155, -27.52281430457070499, 5.000000000000000000 ) ) ;
#29482=LINE ( 'NONE', #73717, #30155 ) ;
#29483=VECTOR ( 'NONE', #78594, 999.9999999999998863 ) ;
#29485=CARTESIAN_POINT ( 'NONE',  ( -17.99999999999986855, -19.06887692260762179, 4.000000000000000000 ) ) ;
#29486=ORIENTED_EDGE ( 'NONE', *, *, #140798, .T. ) ;
#29487=EDGE_CURVE ( 'NONE', #138729, #13798, #94989, .T. ) ;
#29488=ORIENTED_EDGE ( 'NONE', *, *, #125044, .T. ) ;
#29489=ORIENTED_EDGE ( 'NONE', *, *, #51248, .T. ) ;
#29491=AXIS2_PLACEMENT_3D ( 'NONE', #1795, #46837, #56278 ) ;
#29493=ADVANCED_FACE ( 'NONE', ( #65993 ), #12280, .F. ) ;
#29494=DIRECTION ( 'NONE',  ( 0.6830127018922180770, -0.6830127018922204085, -0.2588190451025213501 ) ) ;
#29497=VERTEX_POINT ( 'NONE', #77575 ) ;
#29498=LINE ( 'NONE', #117912, #27463 ) ;
#29500=LINE ( 'NONE', #50557, #3917 ) ;
#29501=VECTOR ( 'NONE', #143551, 1000.000000000000227 ) ;
#29502=CARTESIAN_POINT ( 'NONE',  ( -19.49999999999986144, -20.53675388469232388, 2.352720554255848473 ) ) ;
#29504=ORIENTED_EDGE ( 'NONE', *, *, #36629, .F. ) ;
#29505=CARTESIAN_POINT ( 'NONE',  ( -0.4892135623730947680, -27.52281430457055578, 5.000000000000000000 ) ) ;
#29506=LINE ( 'NONE', #87485, #27991 ) ;
#29507=VECTOR ( 'NONE', #3456, 1000.000000000000000 ) ;
#29508=ORIENTED_EDGE ( 'NONE', *, *, #14514, .T. ) ;
#29509=CARTESIAN_POINT ( 'NONE',  ( -9.707106781186462641, -15.74070752338412760, 5.000000000000000000 ) ) ;
#29510=ORIENTED_EDGE ( 'NONE', *, *, #137017, .F. ) ;
#29511=ADVANCED_FACE ( 'NONE', ( #10830 ), #35513, .F. ) ;
#29515=ORIENTED_EDGE ( 'NONE', *, *, #58435, .F. ) ;
#29516=VERTEX_POINT ( 'NONE', #78276 ) ;
#29517=DIRECTION ( 'NONE',  ( -0.7071067811865487940, 0.7071067811865463515, -0.000000000000000000 ) ) ;
#29519=VECTOR ( 'NONE', #105796, 1000.000000000000000 ) ;
#29521=CARTESIAN_POINT ( 'NONE',  ( -24.48921356237309510, -27.52281430457072631, 5.000000000000000000 ) ) ;
#29522=FACE_OUTER_BOUND ( 'NONE', #48888, .T. ) ;
#29523=FACE_OUTER_BOUND ( 'NONE', #62583, .T. ) ;
#29524=CARTESIAN_POINT ( 'NONE',  ( -34.92500000000001137, 3.701285051063773146, 12.01932804697901069 ) ) ;
#29525=CARTESIAN_POINT ( 'NONE',  ( 39.18398860626899705, 28.73617430169814568, 5.000000000000000000 ) ) ;
#29526=DIRECTION ( 'NONE',  ( -0.000000000000000000, 0.000000000000000000, 1.000000000000000000 ) ) ;
#29528=ORIENTED_EDGE ( 'NONE', *, *, #73192, .F. ) ;
#29529=DIRECTION ( 'NONE',  ( -0.000000000000000000, 0.000000000000000000, 1.000000000000000000 ) ) ;
#29530=FACE_OUTER_BOUND ( 'NONE', #110773, .T. ) ;
#29531=ORIENTED_EDGE ( 'NONE', *, *, #26154, .T. ) ;
#29533=VERTEX_POINT ( 'NONE', #44974 ) ;
#29534=EDGE_CURVE ( 'NONE', #5176, #16100, #34062, .T. ) ;
#29535=ORIENTED_EDGE ( 'NONE', *, *, #2538, .T. ) ;
#29537=EDGE_CURVE ( 'NONE', #15997, #123054, #67412, .T. ) ;
#29538=PLANE ( 'NONE',  #39959 ) ;
#29540=VECTOR ( 'NONE', #52672, 1000.000000000000000 ) ;
#29541=CARTESIAN_POINT ( 'NONE',  ( 29.29289321881325137, -15.74070752338412049, 5.000000000000000000 ) ) ;
#29542=ADVANCED_FACE ( 'NONE', ( #44228 ), #90579, .F. ) ;
#29546=VECTOR ( 'NONE', #138470, 1000.000000000000227 ) ;
#29547=VECTOR ( 'NONE', #10936, 1000.000000000000000 ) ;
#29548=EDGE_CURVE ( 'NONE', #5611, #2635, #681, .T. ) ;
#29551=CARTESIAN_POINT ( 'NONE',  ( 34.49999999999975842, 1.464255608400477415, 4.994342998332161443 ) ) ;
#29552=EDGE_CURVE ( 'NONE', #131572, #138628, #56566, .T. ) ;
#29553=DIRECTION ( 'NONE',  ( 0.6830127018922181881, 0.6830127018922202975, -0.2588190451025214056 ) ) ;
#29554=CARTESIAN_POINT ( 'NONE',  ( 32.99999999999977973, 7.588810512006247677, -3.013526669885301601 ) ) ;
#29555=ORIENTED_EDGE ( 'NONE', *, *, #74468, .T. ) ;
#29557=ADVANCED_FACE ( 'NONE', ( #24585 ), #89149, .T. ) ;
#29558=ORIENTED_EDGE ( 'NONE', *, *, #131646, .F. ) ;
#29559=LINE ( 'NONE', #73797, #23248 ) ;
#29560=DIRECTION ( 'NONE',  ( 1.000000000000000000, 0.000000000000000000, 0.000000000000000000 ) ) ;
#29562=DIRECTION ( 'NONE',  ( -0.000000000000000000, -0.3543493200069152693, 0.9351131265310292928 ) ) ;
#29563=DIRECTION ( 'NONE',  ( 1.000000000000000000, 0.000000000000000000, 0.000000000000000000 ) ) ;
#29565=DIRECTION ( 'NONE',  ( 0.7071067811865486830, -0.7071067811865464625, -0.000000000000000000 ) ) ;
#29566=LINE ( 'NONE', #98926, #69635 ) ;
#29567=EDGE_CURVE ( 'NONE', #56571, #136567, #122459, .T. ) ;
#29568=LINE ( 'NONE', #15113, #108719 ) ;
#29570=CARTESIAN_POINT ( 'NONE',  ( -12.71757738642558877, -21.73023691814493219, 5.000000000000000888 ) ) ;
#29571=CARTESIAN_POINT ( 'NONE',  ( -15.29974487139158867, -27.71228299555216879, 4.000000000000000000 ) ) ;
#29572=ORIENTED_EDGE ( 'NONE', *, *, #112869, .T. ) ;
#29574=PLANE ( 'NONE',  #91031 ) ;
#29575=ORIENTED_EDGE ( 'NONE', *, *, #109785, .F. ) ;
#29577=CARTESIAN_POINT ( 'NONE',  ( 24.70612307739177638, 22.22500000000000142, 4.000000000000000000 ) ) ;
#29579=VERTEX_POINT ( 'NONE', #89836 ) ;
#29580=EDGE_CURVE ( 'NONE', #20842, #137446, #134079, .T. ) ;
#29581=CARTESIAN_POINT ( 'NONE',  ( -33.29974487139158867, -27.71228299555229313, 4.000000000000000000 ) ) ;
#29582=CARTESIAN_POINT ( 'NONE',  ( 18.18398860626898994, 28.73617430169800002, 5.000000000000000000 ) ) ;
#29583=AXIS2_PLACEMENT_3D ( 'NONE', #106525, #74670, #20963 ) ;
#29584=ORIENTED_EDGE ( 'NONE', *, *, #53389, .T. ) ;
#29585=CARTESIAN_POINT ( 'NONE',  ( 36.48921356237310221, -27.52281430457080802, 5.000000000000000000 ) ) ;
#29590=CARTESIAN_POINT ( 'NONE',  ( 75.18398860626899705, 28.73617430169839793, 5.000000000000000000 ) ) ;
#29591=DIRECTION ( 'NONE',  ( -0.3543493200069162685, -0.000000000000000000, -0.9351131265310288487 ) ) ;
#29592=PLANE ( 'NONE',  #35227 ) ;
#29594=DIRECTION ( 'NONE',  ( 0.6830127018922181881, 0.6830127018922202975, -0.2588190451025214056 ) ) ;
#29597=CARTESIAN_POINT ( 'NONE',  ( -10.49999999999992895, -2.568876922607790103, 4.000000000000000000 ) ) ;
#29598=CARTESIAN_POINT ( 'NONE',  ( -51.18398860626899705, 28.73617430169823095, 5.000000000000000000 ) ) ;
#29599=ORIENTED_EDGE ( 'NONE', *, *, #7723, .F. ) ;
#29600=EDGE_LOOP ( 'NONE', ( #19892, #75067, #117680, #49657 ) ) ;
#29602=ORIENTED_EDGE ( 'NONE', *, *, #59534, .F. ) ;
#29604=EDGE_CURVE ( 'NONE', #17816, #134787, #123927, .T. ) ;
#29605=DIRECTION ( 'NONE',  ( 0.7071067811865487940, 0.7071067811865463515, 0.000000000000000000 ) ) ;
#29606=DIRECTION ( 'NONE',  ( 0.7071067811865486830, -0.7071067811865464625, -0.000000000000000000 ) ) ;
#29608=PLANE ( 'NONE',  #68616 ) ;
#29609=VERTEX_POINT ( 'NONE', #71676 ) ;
#29610=PLANE ( 'NONE',  #88084 ) ;
#29612=AXIS2_PLACEMENT_3D ( 'NONE', #30971, #119356, #42571 ) ;
#29614=PLANE ( 'NONE',  #31316 ) ;
#29615=ORIENTED_EDGE ( 'NONE', *, *, #8612, .F. ) ;
#29616=PLANE ( 'NONE',  #44334 ) ;
#29618=CARTESIAN_POINT ( 'NONE',  ( -39.18398860626899705, 28.73617430169814568, 5.000000000000000000 ) ) ;
#29619=LINE ( 'NONE', #5717, #57040 ) ;
#29620=CARTESIAN_POINT ( 'NONE',  ( 22.49999999999985789, 16.08746187583907883, 4.000000000000000000 ) ) ;
#29621=EDGE_CURVE ( 'NONE', #667, #79851, #4929, .T. ) ;
#29623=ORIENTED_EDGE ( 'NONE', *, *, #79236, .F. ) ;
#29624=ORIENTED_EDGE ( 'NONE', *, *, #48464, .T. ) ;
#29627=ORIENTED_EDGE ( 'NONE', *, *, #112761, .F. ) ;
#29628=EDGE_CURVE ( 'NONE', #136197, #43029, #49933, .T. ) ;
#29629=PLANE ( 'NONE',  #29401 ) ;
#29631=ORIENTED_EDGE ( 'NONE', *, *, #89192, .F. ) ;
#29632=CARTESIAN_POINT ( 'NONE',  ( 54.18398860626899705, 28.73617430169825226, 5.000000000000000000 ) ) ;
#29633=DIRECTION ( 'NONE',  ( 0.6830127018922181881, 0.6830127018922202975, -0.2588190451025214056 ) ) ;
#29636=ADVANCED_FACE ( 'NONE', ( #2828 ), #115843, .F. ) ;
#29637=LINE ( 'NONE', #28240, #81348 ) ;
#29638=ORIENTED_EDGE ( 'NONE', *, *, #29580, .F. ) ;
#29639=FACE_OUTER_BOUND ( 'NONE', #137114, .T. ) ;
#29640=CARTESIAN_POINT ( 'NONE',  ( 4.499999999999968914, 10.94296225409027379, -9.576120664313247488 ) ) ;
#29642=CARTESIAN_POINT ( 'NONE',  ( 19.05000000000000071, 3.174999999999997158, 5.000000000000000000 ) ) ;
#29643=ORIENTED_EDGE ( 'NONE', *, *, #17224, .T. ) ;
#29644=EDGE_LOOP ( 'NONE', ( #83248, #47634, #77261, #73022 ) ) ;
#29645=VECTOR ( 'NONE', #20576, 1000.000000000000000 ) ;
#29646=ADVANCED_FACE ( 'NONE', ( #91307 ), #15115, .T. ) ;
#29647=ORIENTED_EDGE ( 'NONE', *, *, #75452, .T. ) ;
#29648=FACE_OUTER_BOUND ( 'NONE', #8610, .T. ) ;
#29649=LINE ( 'NONE', #113276, #59294 ) ;
#29651=VECTOR ( 'NONE', #37938, 1000.000000000000000 ) ;
#29652=VECTOR ( 'NONE', #76067, 1000.000000000000000 ) ;
#29654=ADVANCED_FACE ( 'NONE', ( #39035 ), #38330, .F. ) ;
#29655=ORIENTED_EDGE ( 'NONE', *, *, #23138, .T. ) ;
#29656=ORIENTED_EDGE ( 'NONE', *, *, #41416, .T. ) ;
#29657=EDGE_CURVE ( 'NONE', #100403, #57736, #49228, .T. ) ;
#29658=DIRECTION ( 'NONE',  ( -0.7071067811865487940, 0.7071067811865463515, 0.000000000000000000 ) ) ;
#29660=ORIENTED_EDGE ( 'NONE', *, *, #100978, .F. ) ;
#29661=EDGE_CURVE ( 'NONE', #8834, #130638, #136203, .T. ) ;
#29662=CARTESIAN_POINT ( 'NONE',  ( -24.29974487139158867, -27.71228299555223273, 4.000000000000000000 ) ) ;
#29663=CARTESIAN_POINT ( 'NONE',  ( 2.671830600776457398, 17.25929247661554911, 4.000000000000000000 ) ) ;
#29664=EDGE_CURVE ( 'NONE', #54301, #86260, #136093, .T. ) ;
#29667=CARTESIAN_POINT ( 'NONE',  ( -32.24139925780183091, 21.72499999999999432, 5.000000000000000000 ) ) ;
#29668=CARTESIAN_POINT ( 'NONE',  ( 50.99451991528749062, 28.92564299267973738, 4.000000000000000000 ) ) ;
#29669=VECTOR ( 'NONE', #68869, 1000.000000000000000 ) ;
#29671=CARTESIAN_POINT ( 'NONE',  ( -34.92500000000001137, 7.512461875839426817, 4.000000000000000000 ) ) ;
#29673=VECTOR ( 'NONE', #24245, 1000.000000000000000 ) ;
#29674=CARTESIAN_POINT ( 'NONE',  ( -59.99451991528749772, 28.92564299267980132, 4.000000000000000000 ) ) ;
#29675=FACE_BOUND ( 'NONE', #105958, .T. ) ;
#29676=VERTEX_POINT ( 'NONE', #81135 ) ;
#29677=LINE ( 'NONE', #84115, #117568 ) ;
#29678=DIRECTION ( 'NONE',  ( 1.000000000000000000, 0.000000000000000000, 0.000000000000000000 ) ) ;
#29679=LINE ( 'NONE', #74655, #127872 ) ;
#29680=ADVANCED_FACE ( 'NONE', ( #125341 ), #47122, .F. ) ;
#29681=EDGE_LOOP ( 'NONE', ( #63230, #32959, #135557, #123872 ) ) ;
#29682=DIRECTION ( 'NONE',  ( 0.7071067811865486830, -0.7071067811865464625, -0.000000000000000000 ) ) ;
#29684=AXIS2_PLACEMENT_3D ( 'NONE', #68105, #10786, #98535 ) ;
#29685=VERTEX_POINT ( 'NONE', #83258 ) ;
#29686=ORIENTED_EDGE ( 'NONE', *, *, #7806, .T. ) ;
#29687=CARTESIAN_POINT ( 'NONE',  ( 60.18398860626900415, 28.73617430169829490, 5.000000000000000000 ) ) ;
#29688=DIRECTION ( 'NONE',  ( 0.7071067811865487940, 0.7071067811865463515, -0.000000000000000000 ) ) ;
#29689=FACE_OUTER_BOUND ( 'NONE', #48567, .T. ) ;
#29690=CARTESIAN_POINT ( 'NONE',  ( -14.99999999999989519, -7.447814304570749222, 5.000000000000000000 ) ) ;
#29692=CARTESIAN_POINT ( 'NONE',  ( -1.828169399223514624, -14.24070752338414181, 4.000000000000000000 ) ) ;
#29693=DIRECTION ( 'NONE',  ( -0.7071067811865486830, -0.7071067811865464625, -0.000000000000000000 ) ) ;
#29695=DIRECTION ( 'NONE',  ( 0.6830127018922180770, -0.6830127018922204085, -0.2588190451025213501 ) ) ;
#29697=CARTESIAN_POINT ( 'NONE',  ( 60.48921356237309510, -27.52281430457097500, 5.000000000000000000 ) ) ;
#29698=LINE ( 'NONE', #63797, #114179 ) ;
#29699=EDGE_LOOP ( 'NONE', ( #37946, #79610, #31482, #87488 ) ) ;
#29701=ORIENTED_EDGE ( 'NONE', *, *, #101511, .T. ) ;
#29702=ORIENTED_EDGE ( 'NONE', *, *, #55511, .F. ) ;
#29703=DIRECTION ( 'NONE',  ( 0.7071067811865487940, -0.7071067811865463515, 0.000000000000000000 ) ) ;
#29707=LINE ( 'NONE', #118133, #50114 ) ;
#29708=DIRECTION ( 'NONE',  ( 0.7071067811865486830, -0.7071067811865464625, -0.000000000000000000 ) ) ;
#29709=LINE ( 'NONE', #128349, #39399 ) ;
#29710=ORIENTED_EDGE ( 'NONE', *, *, #47432, .F. ) ;
#29711=DIRECTION ( 'NONE',  ( -0.7071067811865486830, -0.7071067811865464625, 0.000000000000000000 ) ) ;
#29712=ORIENTED_EDGE ( 'NONE', *, *, #69198, .T. ) ;
#29713=LINE ( 'NONE', #118140, #79141 ) ;
#29714=DIRECTION ( 'NONE',  ( 1.000000000000000000, 0.000000000000000000, -0.000000000000000000 ) ) ;
#29715=ADVANCED_FACE ( 'NONE', ( #25290 ), #47812, .T. ) ;
#29717=ORIENTED_EDGE ( 'NONE', *, *, #9965, .F. ) ;
#29720=EDGE_CURVE ( 'NONE', #6499, #20344, #124618, .T. ) ;
#29722=DIRECTION ( 'NONE',  ( -0.000000000000000000, 0.3543493200069153248, 0.9351131265310292928 ) ) ;
#29724=ORIENTED_EDGE ( 'NONE', *, *, #82626, .T. ) ;
#29725=EDGE_CURVE ( 'NONE', #142121, #110593, #57975, .T. ) ;
#29727=ORIENTED_EDGE ( 'NONE', *, *, #122540, .T. ) ;
#29728=DIRECTION ( 'NONE',  ( -0.7071067811865486830, 0.7071067811865464625, 0.000000000000000000 ) ) ;
#29730=DIRECTION ( 'NONE',  ( -0.7071067811865486830, -0.7071067811865464625, -0.000000000000000000 ) ) ;
#29731=EDGE_CURVE ( 'NONE', #70701, #86413, #13682, .T. ) ;
#29732=DIRECTION ( 'NONE',  ( 0.3543493200069162685, -0.000000000000000000, -0.9351131265310288487 ) ) ;
#29733=ORIENTED_EDGE ( 'NONE', *, *, #32369, .F. ) ;
#29734=FACE_OUTER_BOUND ( 'NONE', #129030, .T. ) ;
#29736=CARTESIAN_POINT ( 'NONE',  ( -6.098435806082331823, 11.25929247661560240, 10.79108189686405872 ) ) ;
#29740=VECTOR ( 'NONE', #25277, 1000.000000000000000 ) ;
#29741=VECTOR ( 'NONE', #85651, 1000.000000000000000 ) ;
#29742=DIRECTION ( 'NONE',  ( 0.7071067811865487940, 0.7071067811865463515, 0.000000000000000000 ) ) ;
#29743=VERTEX_POINT ( 'NONE', #103555 ) ;
#29744=VECTOR ( 'NONE', #96508, 999.9999999999998863 ) ;
#29745=EDGE_CURVE ( 'NONE', #54925, #47459, #48481, .T. ) ;
#29747=VERTEX_POINT ( 'NONE', #26729 ) ;
#29748=ORIENTED_EDGE ( 'NONE', *, *, #39053, .T. ) ;
#29749=ADVANCED_FACE ( 'NONE', ( #60838 ), #115127, .F. ) ;
#29750=AXIS2_PLACEMENT_3D ( 'NONE', #105682, #50623, #28877 ) ;
#29751=LINE ( 'NONE', #64539, #139628 ) ;
#29752=FACE_OUTER_BOUND ( 'NONE', #35387, .T. ) ;
#29754=ORIENTED_EDGE ( 'NONE', *, *, #102088, .T. ) ;
#29755=CARTESIAN_POINT ( 'NONE',  ( -8.510786437626906675, -27.52281430457049183, 5.000000000000000000 ) ) ;
#29757=FACE_OUTER_BOUND ( 'NONE', #109019, .T. ) ;
#29758=FACE_OUTER_BOUND ( 'NONE', #78666, .T. ) ;
#29760=DIRECTION ( 'NONE',  ( 0.7071067811865486830, -0.7071067811865464625, -0.000000000000000000 ) ) ;
#29761=LINE ( 'NONE', #50829, #63330 ) ;
#29762=CARTESIAN_POINT ( 'NONE',  ( -60.18398860626900415, 28.73617430169829490, 5.000000000000000000 ) ) ;
#29763=EDGE_CURVE ( 'NONE', #30212, #126336, #86116, .T. ) ;
#29764=DIRECTION ( 'NONE',  ( 0.6830127018922180770, -0.6830127018922204085, -0.2588190451025213501 ) ) ;
#29765=DIRECTION ( 'NONE',  ( -0.7071067811865486830, -0.7071067811865464625, 0.000000000000000000 ) ) ;
#29767=CARTESIAN_POINT ( 'NONE',  ( -69.18398860626899705, 28.73617430169835529, 5.000000000000000000 ) ) ;
#29770=ORIENTED_EDGE ( 'NONE', *, *, #54833, .F. ) ;
#29772=VECTOR ( 'NONE', #126427, 1000.000000000000227 ) ;
#29775=ORIENTED_EDGE ( 'NONE', *, *, #102783, .T. ) ;
#29776=EDGE_CURVE ( 'NONE', #140087, #3810, #128889, .T. ) ;
#29777=FACE_OUTER_BOUND ( 'NONE', #94969, .T. ) ;
#29778=VECTOR ( 'NONE', #45000, 1000.000000000000000 ) ;
#29780=ORIENTED_EDGE ( 'NONE', *, *, #124531, .T. ) ;
#29781=AXIS2_PLACEMENT_3D ( 'NONE', #106638, #118963, #125218 ) ;
#29782=FACE_OUTER_BOUND ( 'NONE', #27020, .T. ) ;
#29783=VECTOR ( 'NONE', #123765, 1000.000000000000000 ) ;
#29784=DIRECTION ( 'NONE',  ( -0.7071067811865486830, -0.7071067811865464625, 0.000000000000000000 ) ) ;
#29785=VECTOR ( 'NONE', #139935, 1000.000000000000000 ) ;
#29786=CARTESIAN_POINT ( 'NONE',  ( 34.92499999999998295, 22.22500000000000142, 4.000000000000000000 ) ) ;
#29789=EDGE_LOOP ( 'NONE', ( #11365, #116060, #127389, #135017 ) ) ;
#29792=PLANE ( 'NONE',  #89074 ) ;
#29795=LINE ( 'NONE', #69231, #54454 ) ;
#29796=LINE ( 'NONE', #50856, #77046 ) ;
#29797=DIRECTION ( 'NONE',  ( 0.7071067811865487940, 0.7071067811865463515, 0.000000000000000000 ) ) ;
#29798=VECTOR ( 'NONE', #12223, 999.9999999999998863 ) ;
#29800=EDGE_CURVE ( 'NONE', #127400, #22127, #116595, .T. ) ;
#29803=EDGE_LOOP ( 'NONE', ( #97232, #4158, #123686, #47357 ) ) ;
#29804=EDGE_LOOP ( 'NONE', ( #91972, #74213, #29, #84468 ) ) ;
#29806=ORIENTED_EDGE ( 'NONE', *, *, #83858, .T. ) ;
#29811=CARTESIAN_POINT ( 'NONE',  ( -14.81601139373099585, 28.73617430169776910, 5.000000000000000000 ) ) ;
#29812=FACE_OUTER_BOUND ( 'NONE', #58803, .T. ) ;
#29813=FACE_OUTER_BOUND ( 'NONE', #125283, .T. ) ;
#29816=EDGE_CURVE ( 'NONE', #93380, #111380, #7074, .T. ) ;
#29817=LINE ( 'NONE', #61095, #66442 ) ;
#29818=VERTEX_POINT ( 'NONE', #41903 ) ;
#29819=PLANE ( 'NONE',  #139903 ) ;
#29820=DIRECTION ( 'NONE',  ( -0.7071067811865487940, 0.7071067811865463515, -0.000000000000000000 ) ) ;
#29822=DIRECTION ( 'NONE',  ( -0.6830127018922180770, -0.6830127018922204085, -0.2588190451025213501 ) ) ;
#29823=ORIENTED_EDGE ( 'NONE', *, *, #36955, .F. ) ;
#29826=EDGE_LOOP ( 'NONE', ( #89341, #114798, #140031, #3116 ) ) ;
#29827=CARTESIAN_POINT ( 'NONE',  ( -6.489213562373093325, -27.52281430457059841, 5.000000000000000000 ) ) ;
#29828=FACE_OUTER_BOUND ( 'NONE', #94057, .T. ) ;
#29829=FACE_OUTER_BOUND ( 'NONE', #57834, .T. ) ;
#29835=VERTEX_POINT ( 'NONE', #73118 ) ;
#29836=EDGE_LOOP ( 'NONE', ( #117612, #57748, #93565, #108450 ) ) ;
#29837=ORIENTED_EDGE ( 'NONE', *, *, #8883, .F. ) ;
#29838=CARTESIAN_POINT ( 'NONE',  ( -20.99999999999985079, -9.033600742197641864, 5.000000000000000000 ) ) ;
#29839=EDGE_CURVE ( 'NONE', #94364, #13154, #141947, .T. ) ;
#29840=ORIENTED_EDGE ( 'NONE', *, *, #58485, .F. ) ;
#29841=CARTESIAN_POINT ( 'NONE',  ( -36.18398860626899705, 28.73617430169812437, 5.000000000000000000 ) ) ;
#29842=VECTOR ( 'NONE', #142888, 1000.000000000000000 ) ;
#29843=CARTESIAN_POINT ( 'NONE',  ( 6.473360963642107890, -5.240707523384232402, 16.25846745537497284 ) ) ;
#29844=AXIS2_PLACEMENT_3D ( 'NONE', #9718, #120609, #20593 ) ;
#29847=CARTESIAN_POINT ( 'NONE',  ( -0.2997448713915885632, -27.71228299555206220, 4.000000000000000000 ) ) ;
#29849=EDGE_CURVE ( 'NONE', #83015, #81768, #63673, .T. ) ;
#29850=FACE_BOUND ( 'NONE', #59290, .T. ) ;
#29851=ORIENTED_EDGE ( 'NONE', *, *, #15382, .F. ) ;
#29853=CARTESIAN_POINT ( 'NONE',  ( 25.17183060077629619, -17.24070752338410273, 4.000000000000000000 ) ) ;
#29854=DIRECTION ( 'NONE',  ( -0.7071067811865487940, 0.7071067811865463515, -0.000000000000000000 ) ) ;
#29855=EDGE_CURVE ( 'NONE', #15784, #39873, #20114, .T. ) ;
#29856=EDGE_LOOP ( 'NONE', ( #24170, #22059, #134906, #117188 ) ) ;
#29859=VECTOR ( 'NONE', #51548, 1000.000000000000000 ) ;
#29860=DIRECTION ( 'NONE',  ( -0.7071067811865486830, -0.7071067811865464625, 0.000000000000000000 ) ) ;
#29861=VERTEX_POINT ( 'NONE', #72427 ) ;
#29863=VERTEX_POINT ( 'NONE', #117281 ) ;
#29864=CARTESIAN_POINT ( 'NONE',  ( 17.99999999999986855, -19.22509904557634997, 1.855685503482220833 ) ) ;
#29865=DIRECTION ( 'NONE',  ( 0.6830127018922180770, -0.6830127018922204085, -0.2588190451025213501 ) ) ;
#29866=ORIENTED_EDGE ( 'NONE', *, *, #37929, .F. ) ;
#29868=AXIS2_PLACEMENT_3D ( 'NONE', #57265, #87723, #57988 ) ;
#29869=ADVANCED_FACE ( 'NONE', ( #62235 ), #43328, .T. ) ;
#29870=VECTOR ( 'NONE', #113970, 1000.000000000000227 ) ;
#29871=DIRECTION ( 'NONE',  ( -0.6830127018922180770, -0.6830127018922204085, -0.2588190451025213501 ) ) ;
#29872=CARTESIAN_POINT ( 'NONE',  ( 2.700255128608413990, -27.71228299555204089, 4.000000000000000000 ) ) ;
#29874=DIRECTION ( 'NONE',  ( 0.3543493200069162685, -0.000000000000000000, -0.9351131265310288487 ) ) ;
#29875=PLANE ( 'NONE',  #57840 ) ;
#29876=ORIENTED_EDGE ( 'NONE', *, *, #44927, .F. ) ;
#29877=ORIENTED_EDGE ( 'NONE', *, *, #60246, .T. ) ;
#29878=LINE ( 'NONE', #105997, #70574 ) ;
#29879=FACE_OUTER_BOUND ( 'NONE', #4712, .T. ) ;
#29880=VERTEX_POINT ( 'NONE', #99837 ) ;
#29881=VECTOR ( 'NONE', #12654, 1000.000000000000000 ) ;
#29882=EDGE_LOOP ( 'NONE', ( #37739, #56506, #120323, #82621 ) ) ;
#29884=VERTEX_POINT ( 'NONE', #112162 ) ;
#29887=LINE ( 'NONE', #74132, #131804 ) ;
#29888=ORIENTED_EDGE ( 'NONE', *, *, #95606, .T. ) ;
#29889=AXIS2_PLACEMENT_3D ( 'NONE', #31599, #141050, #30896 ) ;
#29890=CARTESIAN_POINT ( 'NONE',  ( 7.171830600776424092, 6.759292476615643253, 4.000000000000000000 ) ) ;
#29891=VECTOR ( 'NONE', #122619, 1000.000000000000000 ) ;
#29893=ADVANCED_FACE ( 'NONE', ( #44799 ), #75949, .F. ) ;
#29895=EDGE_CURVE ( 'NONE', #90863, #52679, #65831, .T. ) ;
#29896=FACE_OUTER_BOUND ( 'NONE', #109259, .T. ) ;
#29897=EDGE_LOOP ( 'NONE', ( #125378, #27506, #98502, #17422 ) ) ;
#29900=DIRECTION ( 'NONE',  ( 0.6830127018922180770, -0.6830127018922204085, -0.2588190451025213501 ) ) ;
#29901=LINE ( 'NONE', #87154, #100477 ) ;
#29903=LINE ( 'NONE', #21891, #84243 ) ;
#29904=ORIENTED_EDGE ( 'NONE', *, *, #41684, .F. ) ;
#29905=CARTESIAN_POINT ( 'NONE',  ( 24.48921356237309510, -27.52281430457072631, 5.000000000000000000 ) ) ;
#29906=VERTEX_POINT ( 'NONE', #78103 ) ;
#29907=CARTESIAN_POINT ( 'NONE',  ( -57.48921356237308800, -27.52281430457095368, 5.000000000000000000 ) ) ;
#29909=EDGE_CURVE ( 'NONE', #26438, #60276, #98418, .T. ) ;
#29910=EDGE_CURVE ( 'NONE', #72227, #18068, #86007, .T. ) ;
#29911=PLANE ( 'NONE',  #10100 ) ;
#29912=ORIENTED_EDGE ( 'NONE', *, *, #134037, .F. ) ;
#29913=DIRECTION ( 'NONE',  ( -0.000000000000000000, -0.3543493200069152693, 0.9351131265310292928 ) ) ;
#29914=DIRECTION ( 'NONE',  ( -0.6830127018922181881, 0.6830127018922202975, -0.2588190451025214056 ) ) ;
#29915=CARTESIAN_POINT ( 'NONE',  ( -18.70710678118641468, -18.74070752338409562, 5.000000000000000000 ) ) ;
#29917=LINE ( 'NONE', #28526, #97091 ) ;
#29918=DIRECTION ( 'NONE',  ( -0.3543493200069162685, -0.000000000000000000, -0.9351131265310288487 ) ) ;
#29919=CYLINDRICAL_SURFACE ( 'NONE', #139816, 0.5000000000000004441 ) ;
#29921=CARTESIAN_POINT ( 'NONE',  ( 16.58990935480158413, 9.759292476615621936, 11.28811694763782469 ) ) ;
#29922=VERTEX_POINT ( 'NONE', #33884 ) ;
#29923=EDGE_CURVE ( 'NONE', #130643, #117951, #10657, .T. ) ;
#29924=ORIENTED_EDGE ( 'NONE', *, *, #12723, .F. ) ;
#29925=LINE ( 'NONE', #74169, #5544 ) ;
#29926=DIRECTION ( 'NONE',  ( 0.7071067811865487940, 0.7071067811865463515, 0.000000000000000000 ) ) ;
#29927=EDGE_CURVE ( 'NONE', #143369, #122228, #54924, .T. ) ;
#29929=DIRECTION ( 'NONE',  ( 1.000000000000000000, 0.000000000000000000, 0.000000000000000000 ) ) ;
#29930=CARTESIAN_POINT ( 'NONE',  ( -3.643187427517367905, -20.24070752338407786, 21.22881796311212099 ) ) ;
#29931=EDGE_CURVE ( 'NONE', #115930, #81209, #88263, .T. ) ;
#29932=CARTESIAN_POINT ( 'NONE',  ( -69.48921356237309510, -27.52281430457103895, 5.000000000000000000 ) ) ;
#29933=ORIENTED_EDGE ( 'NONE', *, *, #39907, .F. ) ;
#29934=LINE ( 'NONE', #115488, #27933 ) ;
#29935=CARTESIAN_POINT ( 'NONE',  ( -27.29974487139158512, -27.71228299555225405, 4.000000000000000000 ) ) ;
#29936=CARTESIAN_POINT ( 'NONE',  ( 6.489213562373093325, -27.52281430457059841, 5.000000000000000000 ) ) ;
#29937=EDGE_CURVE ( 'NONE', #113570, #89814, #54234, .T. ) ;
#29938=PLANE ( 'NONE',  #62228 ) ;
#29940=CARTESIAN_POINT ( 'NONE',  ( -11.70025512860841133, -27.71228299555198049, 4.000000000000000000 ) ) ;
#29941=EDGE_LOOP ( 'NONE', ( #128404, #42915, #139373, #5272 ) ) ;
#29942=CARTESIAN_POINT ( 'NONE',  ( -18.71757738642554258, -21.73023691814492864, 5.000000000000000888 ) ) ;
#29943=EDGE_LOOP ( 'NONE', ( #63941, #34095, #1419, #135090 ) ) ;
#29944=ORIENTED_EDGE ( 'NONE', *, *, #94014, .F. ) ;
#29945=ADVANCED_FACE ( 'NONE', ( #12101 ), #77412, .F. ) ;
#29946=CARTESIAN_POINT ( 'NONE',  ( 32.99999999999977263, -21.41253812416053393, 4.000000000000000000 ) ) ;
#29947=CARTESIAN_POINT ( 'NONE',  ( 28.49999999999980815, 10.46639925780215563, 5.000000000000000000 ) ) ;
#29948=AXIS2_PLACEMENT_3D ( 'NONE', #33328, #55051, #43447 ) ;
#29949=VECTOR ( 'NONE', #35619, 1000.000000000000000 ) ;
#29950=VECTOR ( 'NONE', #122731, 999.9999999999998863 ) ;
#29951=DIRECTION ( 'NONE',  ( -0.7071067811865486830, 0.7071067811865464625, 0.000000000000000000 ) ) ;
#29952=VECTOR ( 'NONE', #15729, 1000.000000000000227 ) ;
#29953=CARTESIAN_POINT ( 'NONE',  ( -45.48921356237309510, -27.52281430457087197, 5.000000000000000000 ) ) ;
#29954=FACE_OUTER_BOUND ( 'NONE', #9019, .T. ) ;
#29955=DIRECTION ( 'NONE',  ( 0.7071067811865486830, -0.7071067811865464625, -0.000000000000000000 ) ) ;
#29956=ORIENTED_EDGE ( 'NONE', *, *, #2424, .T. ) ;
#29957=EDGE_CURVE ( 'NONE', #117951, #107684, #110676, .T. ) ;
#29958=LINE ( 'NONE', #16206, #55677 ) ;
#29960=ADVANCED_FACE ( 'NONE', ( #56386 ), #65095, .F. ) ;
#29961=DIRECTION ( 'NONE',  ( -0.000000000000000000, 0.000000000000000000, 1.000000000000000000 ) ) ;
#29962=VECTOR ( 'NONE', #140498, 1000.000000000000000 ) ;
#29963=PLANE ( 'NONE',  #55487 ) ;
#29964=DIRECTION ( 'NONE',  ( 0.7071067811865487940, 0.7071067811865463515, -0.000000000000000000 ) ) ;
#29965=CARTESIAN_POINT ( 'NONE',  ( -32.99999999999977263, 20.70535890316558536, 1.956823837851992209 ) ) ;
#29967=ADVANCED_FACE ( 'NONE', ( #34591 ), #142635, .F. ) ;
#29968=PLANE ( 'NONE',  #41465 ) ;
#29969=VECTOR ( 'NONE', #54564, 999.9999999999998863 ) ;
#29970=ORIENTED_EDGE ( 'NONE', *, *, #82602, .T. ) ;
#29971=ORIENTED_EDGE ( 'NONE', *, *, #17517, .F. ) ;
#29973=CARTESIAN_POINT ( 'NONE',  ( 3.707106781186524369, -12.74070752338415602, 5.000000000000000000 ) ) ;
#29974=DIRECTION ( 'NONE',  ( 1.000000000000000000, 0.000000000000000000, 0.000000000000000000 ) ) ;
#29976=VECTOR ( 'NONE', #121384, 1000.000000000000000 ) ;
#29977=CARTESIAN_POINT ( 'NONE',  ( 8.292893218813407685, -6.740707523384214639, 5.000000000000000000 ) ) ;
#29980=( BOUNDED_CURVE ( )  B_SPLINE_CURVE ( 3, ( #4546, #84353, #26382, #16925 ),
 .UNSPECIFIED., .F., .T. ) 
 B_SPLINE_CURVE_WITH_KNOTS ( ( 4, 4 ),
 ( 1.739935637444958383, 1.766022064991929819 ),
 .UNSPECIFIED. ) 
 CURVE ( )  GEOMETRIC_REPRESENTATION_ITEM ( )  RATIONAL_B_SPLINE_CURVE ( ( 1.000000000000000000, 0.9999432923287778774, 0.9999432923287778774, 1.000000000000000000 ) ) 
 REPRESENTATION_ITEM ( '' )  );
#29983=ORIENTED_EDGE ( 'NONE', *, *, #110630, .F. ) ;
#29984=LINE ( 'NONE', #141626, #54854 ) ;
#29985=ORIENTED_EDGE ( 'NONE', *, *, #32400, .F. ) ;
#29986=VERTEX_POINT ( 'NONE', #46212 ) ;
#29987=CARTESIAN_POINT ( 'NONE',  ( -34.49999999999975842, -11.94567065516892690, 4.994342998332167660 ) ) ;
#29988=VECTOR ( 'NONE', #24140, 1000.000000000000000 ) ;
#29989=AXIS2_PLACEMENT_3D ( 'NONE', #60489, #51017, #72090 ) ;
#29991=DIRECTION ( 'NONE',  ( -0.6830127018922181881, 0.6830127018922202975, -0.2588190451025214056 ) ) ;
#29994=ORIENTED_EDGE ( 'NONE', *, *, #73352, .F. ) ;
#29995=PLANE ( 'NONE',  #111315 ) ;
#29996=FACE_OUTER_BOUND ( 'NONE', #7422, .T. ) ;
#29997=ORIENTED_EDGE ( 'NONE', *, *, #118909, .T. ) ;
#29998=AXIS2_PLACEMENT_3D ( 'NONE', #119661, #21090, #76943 ) ;
#29999=LINE ( 'NONE', #108974, #27715 ) ;
#30000=DIRECTION ( 'NONE',  ( 0.7071067811865487940, 0.7071067811865463515, -0.000000000000000000 ) ) ;
#30001=FACE_OUTER_BOUND ( 'NONE', #129859, .T. ) ;
#30002=VECTOR ( 'NONE', #128594, 1000.000000000000000 ) ;
#30003=DIRECTION ( 'NONE',  ( -0.7071067811865487940, 0.7071067811865463515, -0.000000000000000000 ) ) ;
#30004=CARTESIAN_POINT ( 'NONE',  ( -45.29974487139158867, -27.71228299555237840, 4.000000000000000000 ) ) ;
#30005=ORIENTED_EDGE ( 'NONE', *, *, #73537, .T. ) ;
#30006=EDGE_LOOP ( 'NONE', ( #136910, #81331, #128308, #55274 ) ) ;
#30008=DIRECTION ( 'NONE',  ( -0.7071067811865486830, -0.7071067811865464625, 0.000000000000000000 ) ) ;
#30009=DIRECTION ( 'NONE',  ( -0.6830127018922180770, -0.6830127018922204085, -0.2588190451025213501 ) ) ;
#30010=PLANE ( 'NONE',  #68707 ) ;
#30011=ORIENTED_EDGE ( 'NONE', *, *, #51678, .F. ) ;
#30012=ORIENTED_EDGE ( 'NONE', *, *, #63536, .F. ) ;
#30013=CARTESIAN_POINT ( 'NONE',  ( -81.48921356237309510, -27.52281430457112066, 5.000000000000000000 ) ) ;
#30014=LINE ( 'NONE', #120568, #111610 ) ;
#30015=VERTEX_POINT ( 'NONE', #87539 ) ;
#30016=EDGE_LOOP ( 'NONE', ( #47138, #47136, #73099, #55870 ) ) ;
#30017=CARTESIAN_POINT ( 'NONE',  ( 34.49999999999975131, 13.46425560840035196, 4.994342998332160555 ) ) ;
#30020=DIRECTION ( 'NONE',  ( -1.000000000000000000, 0.000000000000000000, -0.000000000000000000 ) ) ;
#30021=LINE ( 'NONE', #64824, #76591 ) ;
#30022=EDGE_CURVE ( 'NONE', #138721, #75295, #131047, .T. ) ;
#30023=FACE_BOUND ( 'NONE', #103043, .T. ) ;
#30027=EDGE_CURVE ( 'NONE', #20459, #100121, #20834, .T. ) ;
#30028=CARTESIAN_POINT ( 'NONE',  ( -11.99999999999991296, -15.03360074219758502, 5.000000000000000000 ) ) ;
#30029=PLANE ( 'NONE',  #133875 ) ;
#30033=ORIENTED_EDGE ( 'NONE', *, *, #29047, .T. ) ;
#30034=ORIENTED_EDGE ( 'NONE', *, *, #130710, .T. ) ;
#30036=ORIENTED_EDGE ( 'NONE', *, *, #647, .T. ) ;
#30037=CARTESIAN_POINT ( 'NONE',  ( -22.88982677111772901, -22.22499999999999787, 4.785647885939354751 ) ) ;
#30038=EDGE_CURVE ( 'NONE', #35605, #114108, #47648, .T. ) ;
#30039=PLANE ( 'NONE',  #18781 ) ;
#30040=DIRECTION ( 'NONE',  ( 4.681814790819592407E-17, 0.3543493200069153248, 0.9351131265310292928 ) ) ;
#30041=EDGE_CURVE ( 'NONE', #138878, #32128, #73473, .T. ) ;
#30042=CARTESIAN_POINT ( 'NONE',  ( 9.489213562373095101, -27.52281430457062328, 5.000000000000000000 ) ) ;
#30043=DIRECTION ( 'NONE',  ( -0.6830127018922180770, -0.6830127018922204085, -0.2588190451025213501 ) ) ;
#30044=PLANE ( 'NONE',  #33905 ) ;
#30045=CARTESIAN_POINT ( 'NONE',  ( 42.48921356237308800, -27.52281430457085065, 5.000000000000000000 ) ) ;
#30046=FACE_OUTER_BOUND ( 'NONE', #12072, .T. ) ;
#30048=AXIS2_PLACEMENT_3D ( 'NONE', #27695, #18968, #116133 ) ;
#30049=VECTOR ( 'NONE', #113886, 1000.000000000000000 ) ;
#30050=ADVANCED_FACE ( 'NONE', ( #16941 ), #101982, .F. ) ;
#30051=AXIS2_PLACEMENT_3D ( 'NONE', #77394, #103363, #102693 ) ;
#30052=DIRECTION ( 'NONE',  ( 1.000000000000000000, 0.000000000000000000, 0.000000000000000000 ) ) ;
#30053=VECTOR ( 'NONE', #119153, 1000.000000000000000 ) ;
#30054=ORIENTED_EDGE ( 'NONE', *, *, #50418, .F. ) ;
#30055=DIRECTION ( 'NONE',  ( -0.000000000000000000, -0.3543493200069152693, 0.9351131265310292928 ) ) ;
#30056=CARTESIAN_POINT ( 'NONE',  ( -30.79333936457826226, 21.75929247661549581, 4.998822639870701856 ) ) ;
#30058=ORIENTED_EDGE ( 'NONE', *, *, #114485, .T. ) ;
#30059=ORIENTED_EDGE ( 'NONE', *, *, #25553, .F. ) ;
#30062=EDGE_CURVE ( 'NONE', #40404, #106314, #6719, .T. ) ;
#30063=ORIENTED_EDGE ( 'NONE', *, *, #103061, .T. ) ;
#30064=AXIS2_PLACEMENT_3D ( 'NONE', #101110, #22804, #35900 ) ;
#30065=DIRECTION ( 'NONE',  ( -0.7071067811865486830, -0.7071067811865464625, 0.000000000000000000 ) ) ;
#30068=ORIENTED_EDGE ( 'NONE', *, *, #86285, .F. ) ;
#30069=PLANE ( 'NONE',  #36263 ) ;
#30070=EDGE_CURVE ( 'NONE', #57200, #79351, #124446, .T. ) ;
#30071=EDGE_LOOP ( 'NONE', ( #109433, #100101, #126354, #123816 ) ) ;
#30072=DIRECTION ( 'NONE',  ( 0.7071067811865486830, -0.7071067811865464625, -0.000000000000000000 ) ) ;
#30073=VECTOR ( 'NONE', #137142, 1000.000000000000000 ) ;
#30075=LINE ( 'NONE', #137437, #44832 ) ;
#30076=ORIENTED_EDGE ( 'NONE', *, *, #136145, .F. ) ;
#30077=ORIENTED_EDGE ( 'NONE', *, *, #37347, .F. ) ;
#30078=LINE ( 'NONE', #40290, #63093 ) ;
#30080=EDGE_CURVE ( 'NONE', #20632, #71393, #139469, .T. ) ;
#30081=CARTESIAN_POINT ( 'NONE',  ( -66.18398860626901126, 28.73617430169833753, 5.000000000000000000 ) ) ;
#30082=ORIENTED_EDGE ( 'NONE', *, *, #127279, .T. ) ;
#30084=CARTESIAN_POINT ( 'NONE',  ( 23.99451991528749062, 28.92564299267954908, 4.000000000000000000 ) ) ;
#30086=ORIENTED_EDGE ( 'NONE', *, *, #37862, .F. ) ;
#30087=EDGE_LOOP ( 'NONE', ( #28291, #131831, #121480, #57427 ) ) ;
#30088=PLANE ( 'NONE',  #86542 ) ;
#30089=VECTOR ( 'NONE', #57300, 1000.000000000000000 ) ;
#30090=EDGE_CURVE ( 'NONE', #94326, #8586, #2648, .T. ) ;
#30091=DIRECTION ( 'NONE',  ( -0.000000000000000000, -0.3543493200069152693, 0.9351131265310292928 ) ) ;
#30093=LINE ( 'NONE', #74343, #125834 ) ;
#30096=ORIENTED_EDGE ( 'NONE', *, *, #45474, .F. ) ;
#30097=VECTOR ( 'NONE', #24017, 1000.000000000000000 ) ;
#30099=DIRECTION ( 'NONE',  ( -0.7071067811865487940, 0.7071067811865463515, 0.000000000000000000 ) ) ;
#30100=ORIENTED_EDGE ( 'NONE', *, *, #127846, .T. ) ;
#30101=VECTOR ( 'NONE', #92203, 1000.000000000000000 ) ;
#30102=DIRECTION ( 'NONE',  ( 0.3543493200069162685, -0.000000000000000000, -0.9351131265310288487 ) ) ;
#30104=ORIENTED_EDGE ( 'NONE', *, *, #6554, .F. ) ;
#30105=CARTESIAN_POINT ( 'NONE',  ( 22.49999999999984723, 10.46639925780215563, 5.000000000000000000 ) ) ;
#30107=CARTESIAN_POINT ( 'NONE',  ( -6.183988606268994381, 28.73617430169791476, 5.000000000000000000 ) ) ;
#30108=ORIENTED_EDGE ( 'NONE', *, *, #39052, .T. ) ;
#30109=ORIENTED_EDGE ( 'NONE', *, *, #38660, .F. ) ;
#30110=LINE ( 'NONE', #128035, #53274 ) ;
#30111=CARTESIAN_POINT ( 'NONE',  ( 34.92499999999998295, -15.15525166281332581, -9.164774702225022551 ) ) ;
#30112=VECTOR ( 'NONE', #32854, 1000.000000000000227 ) ;
#30113=FACE_OUTER_BOUND ( 'NONE', #129613, .T. ) ;
#30114=DIRECTION ( 'NONE',  ( 0.7071067811865486830, -0.7071067811865464625, -0.000000000000000000 ) ) ;
#30115=EDGE_CURVE ( 'NONE', #142404, #50417, #51003, .T. ) ;
#30118=LINE ( 'NONE', #118555, #44089 ) ;
#30119=CARTESIAN_POINT ( 'NONE',  ( 3.183988606268992161, 28.73617430169789699, 5.000000000000000000 ) ) ;
#30120=DIRECTION ( 'NONE',  ( -0.7071067811865486830, -0.7071067811865464625, 0.000000000000000000 ) ) ;
#30122=ORIENTED_EDGE ( 'NONE', *, *, #115981, .F. ) ;
#30125=VECTOR ( 'NONE', #84, 1000.000000000000227 ) ;
#30127=CARTESIAN_POINT ( 'NONE',  ( -39.29974487139159578, -27.71228299555233576, 4.000000000000000000 ) ) ;
#30128=ORIENTED_EDGE ( 'NONE', *, *, #33259, .F. ) ;
#30129=CARTESIAN_POINT ( 'NONE',  ( 5.999999999999967137, 1.552185695429152856, 5.000000000000000000 ) ) ;
#30131=ORIENTED_EDGE ( 'NONE', *, *, #46163, .T. ) ;
#30132=CARTESIAN_POINT ( 'NONE',  ( -14.99999999999990230, 14.58746187583910192, 4.000000000000000000 ) ) ;
#30133=FACE_OUTER_BOUND ( 'NONE', #114522, .T. ) ;
#30134=DIRECTION ( 'NONE',  ( -0.7071067811865486830, -0.7071067811865464625, -0.000000000000000000 ) ) ;
#30135=ORIENTED_EDGE ( 'NONE', *, *, #7920, .T. ) ;
#30137=CARTESIAN_POINT ( 'NONE',  ( 18.79289321881333663, -8.240707523384195099, 5.000000000000000000 ) ) ;
#30140=VECTOR ( 'NONE', #513, 999.9999999999998863 ) ;
#30141=FACE_OUTER_BOUND ( 'NONE', #41374, .T. ) ;
#30142=EDGE_CURVE ( 'NONE', #49004, #28681, #33267, .T. ) ;
#30144=DIRECTION ( 'NONE',  ( -0.3543493200069162685, -0.000000000000000000, -0.9351131265310288487 ) ) ;
#30145=EDGE_CURVE ( 'NONE', #119189, #83353, #61895, .T. ) ;
#30146=CARTESIAN_POINT ( 'NONE',  ( 28.21321903303341472, 12.75929247661558996, 10.29404684609041887 ) ) ;
#30149=DIRECTION ( 'NONE',  ( 1.000000000000000000, 0.000000000000000000, 0.000000000000000000 ) ) ;
#30151=ORIENTED_EDGE ( 'NONE', *, *, #52827, .T. ) ;
#30152=AXIS2_PLACEMENT_3D ( 'NONE', #73117, #50627, #9205 ) ;
#30153=EDGE_CURVE ( 'NONE', #55970, #22881, #58540, .T. ) ;
#30154=DIRECTION ( 'NONE',  ( -0.000000000000000000, -0.3543493200069152693, 0.9351131265310292928 ) ) ;
#30155=VECTOR ( 'NONE', #94030, 1000.000000000000000 ) ;
#30157=VECTOR ( 'NONE', #30273, 1000.000000000000000 ) ;
#30159=CARTESIAN_POINT ( 'NONE',  ( 5.999999999999961808, -6.412538124160692909, 4.000000000000000000 ) ) ;
#30160=VECTOR ( 'NONE', #105952, 999.9999999999998863 ) ;
#30163=VECTOR ( 'NONE', #69171, 1000.000000000000000 ) ;
#30164=AXIS2_PLACEMENT_3D ( 'NONE', #131402, #120, #122645 ) ;
#30166=DIRECTION ( 'NONE',  ( -0.7071067811865486830, 0.7071067811865464625, 0.000000000000000000 ) ) ;
#30167=VECTOR ( 'NONE', #40446, 1000.000000000000000 ) ;
#30168=CARTESIAN_POINT ( 'NONE',  ( -42.18398860626899705, 28.73617430169816700, 5.000000000000000000 ) ) ;
#30169=CARTESIAN_POINT ( 'NONE',  ( -17.70025512860841488, -27.71228299555193786, 4.000000000000000000 ) ) ;
#30170=CARTESIAN_POINT ( 'NONE',  ( 0.000000000000000000, 0.000000000000000000, 5.000000000000000000 ) ) ;
#30171=CARTESIAN_POINT ( 'NONE',  ( -32.99999999999976552, -3.412538124160721331, 4.000000000000000000 ) ) ;
#30172=VERTEX_POINT ( 'NONE', #17624 ) ;
#30174=CARTESIAN_POINT ( 'NONE',  ( -39.13499573751598604, 3.759292476615678336, 15.36553568819735283 ) ) ;
#30175=CARTESIAN_POINT ( 'NONE',  ( 36.27825451568550363, 8.259292476615637923, 11.78515199841158889 ) ) ;
#30176=VECTOR ( 'NONE', #44277, 1000.000000000000000 ) ;
#30177=LINE ( 'NONE', #83146, #56225 ) ;
#30178=VERTEX_POINT ( 'NONE', #90388 ) ;
#30179=ORIENTED_EDGE ( 'NONE', *, *, #101361, .T. ) ;
#30182=CARTESIAN_POINT ( 'NONE',  ( -0.005480084712502889671, 28.92564299267938210, 4.000000000000000000 ) ) ;
#30183=LINE ( 'NONE', #20730, #140638 ) ;
#30184=VECTOR ( 'NONE', #7077, 1000.000000000000000 ) ;
#30185=CARTESIAN_POINT ( 'NONE',  ( 20.99999999999985079, 8.816494571476654940, 4.604407763760433703 ) ) ;
#30187=EDGE_LOOP ( 'NONE', ( #88104, #124106, #63772, #83031 ) ) ;
#30188=CARTESIAN_POINT ( 'NONE',  ( -3.793339364578453665, 21.75929247661549581, 4.998822639870701856 ) ) ;
#30190=AXIS2_PLACEMENT_3D ( 'NONE', #142720, #43410, #87624 ) ;
#30191=EDGE_LOOP ( 'NONE', ( #131873, #127723, #104674, #49357 ) ) ;
#30193=DIRECTION ( 'NONE',  ( 0.7071067811865487940, 0.7071067811865463515, 0.000000000000000000 ) ) ;
#30194=VECTOR ( 'NONE', #94501, 1000.000000000000000 ) ;
#30195=CARTESIAN_POINT ( 'NONE',  ( -34.92500000000001137, 22.22500000000000142, 4.000000000000000000 ) ) ;
#30196=DIRECTION ( 'NONE',  ( 0.3543493200069162685, -0.000000000000000000, -0.9351131265310288487 ) ) ;
#30197=VECTOR ( 'NONE', #109832, 1000.000000000000000 ) ;
#30198=EDGE_LOOP ( 'NONE', ( #130326, #60135, #61341, #92830 ) ) ;
#30199=ORIENTED_EDGE ( 'NONE', *, *, #71808, .F. ) ;
#30200=EDGE_CURVE ( 'NONE', #109338, #119169, #3357, .T. ) ;
#30203=FACE_BOUND ( 'NONE', #48664, .T. ) ;
#30205=CARTESIAN_POINT ( 'NONE',  ( -17.20710678118642178, 12.75929247661558641, 5.000000000000000000 ) ) ;
#30206=CARTESIAN_POINT ( 'NONE',  ( -29.99999999999979039, 19.93112307739198386, 4.000000000000000000 ) ) ;
#30208=LINE ( 'NONE', #6987, #50374 ) ;
#30209=ADVANCED_FACE ( 'NONE', ( #8168 ), #129984, .F. ) ;
#30210=EDGE_CURVE ( 'NONE', #6460, #67219, #41524, .T. ) ;
#30211=DIRECTION ( 'NONE',  ( 0.7071067811865487940, 0.7071067811865463515, 0.000000000000000000 ) ) ;
#30212=VERTEX_POINT ( 'NONE', #86491 ) ;
#30213=VECTOR ( 'NONE', #36714, 1000.000000000000000 ) ;
#30214=ORIENTED_EDGE ( 'NONE', *, *, #101187, .F. ) ;
#30215=VERTEX_POINT ( 'NONE', #52407 ) ;
#30216=EDGE_CURVE ( 'NONE', #94223, #123054, #141580, .T. ) ;
#30220=LINE ( 'NONE', #75884, #45532 ) ;
#30221=EDGE_CURVE ( 'NONE', #17057, #28238, #30686, .T. ) ;
#30222=CARTESIAN_POINT ( 'NONE',  ( 9.489213562373095101, -27.52281430457062328, 5.000000000000000000 ) ) ;
#30223=ORIENTED_EDGE ( 'NONE', *, *, #7454, .T. ) ;
#30225=DIRECTION ( 'NONE',  ( 0.3543493200069162685, -0.000000000000000000, -0.9351131265310288487 ) ) ;
#30227=CARTESIAN_POINT ( 'NONE',  ( -16.82816939922341959, 9.759292476615618384, 4.000000000000000000 ) ) ;
#30228=VECTOR ( 'NONE', #28325, 1000.000000000000000 ) ;
#30229=EDGE_CURVE ( 'NONE', #79128, #118195, #132142, .T. ) ;
#30230=DIRECTION ( 'NONE',  ( -0.000000000000000000, 0.000000000000000000, 1.000000000000000000 ) ) ;
#30232=DIRECTION ( 'NONE',  ( 0.7071067811865487940, -0.7071067811865463515, 0.000000000000000000 ) ) ;
#30234=ORIENTED_EDGE ( 'NONE', *, *, #4315, .F. ) ;
#30236=VERTEX_POINT ( 'NONE', #130722 ) ;
#30238=ORIENTED_EDGE ( 'NONE', *, *, #114508, .T. ) ;
#30240=EDGE_CURVE ( 'NONE', #7595, #100121, #40835, .T. ) ;
#30241=VECTOR ( 'NONE', #116972, 1000.000000000000000 ) ;
#30242=VERTEX_POINT ( 'NONE', #119095 ) ;
#30244=CARTESIAN_POINT ( 'NONE',  ( -75.18398860626899705, 28.73617430169839793, 5.000000000000000000 ) ) ;
#30245=CARTESIAN_POINT ( 'NONE',  ( 39.48921356237310221, -27.52281430457082934, 5.000000000000000000 ) ) ;
#30247=( BOUNDED_CURVE ( )  B_SPLINE_CURVE ( 3, ( #18611, #104189, #62888, #107072 ),
 .UNSPECIFIED., .F., .T. ) 
 B_SPLINE_CURVE_WITH_KNOTS ( ( 4, 4 ),
 ( 1.964434688349477875, 3.503810798801451742 ),
 .UNSPECIFIED. ) 
 CURVE ( )  GEOMETRIC_REPRESENTATION_ITEM ( )  RATIONAL_B_SPLINE_CURVE ( ( 1.000000000000000000, 0.8120851936182257313, 0.8120851936182257313, 1.000000000000000000 ) ) 
 REPRESENTATION_ITEM ( '' )  );
#30248=FACE_OUTER_BOUND ( 'NONE', #47921, .T. ) ;
#30249=DIRECTION ( 'NONE',  ( 0.7071067811865487940, 0.7071067811865463515, -0.000000000000000000 ) ) ;
#30250=EDGE_CURVE ( 'NONE', #7430, #99882, #97310, .T. ) ;
#30251=DIRECTION ( 'NONE',  ( 0.6830127018922181881, 0.6830127018922202975, -0.2588190451025214056 ) ) ;
#30253=DIRECTION ( 'NONE',  ( 0.6830127018922180770, -0.6830127018922204085, -0.2588190451025213501 ) ) ;
#30254=LINE ( 'NONE', #67182, #39817 ) ;
#30256=FACE_OUTER_BOUND ( 'NONE', #74097, .T. ) ;
#30257=EDGE_CURVE ( 'NONE', #65878, #112121, #65469, .T. ) ;
#30258=VECTOR ( 'NONE', #85818, 1000.000000000000000 ) ;
#30259=VERTEX_POINT ( 'NONE', #19071 ) ;
#30261=ADVANCED_FACE ( 'NONE', ( #85043 ), #63336, .F. ) ;
#30262=EDGE_LOOP ( 'NONE', ( #132774, #100673, #80151, #133707 ) ) ;
#30264=VECTOR ( 'NONE', #85721, 1000.000000000000000 ) ;
#30265=VECTOR ( 'NONE', #104841, 1000.000000000000000 ) ;
#30266=EDGE_LOOP ( 'NONE', ( #30199, #15116, #123405, #93984 ) ) ;
#30268=VECTOR ( 'NONE', #117276, 1000.000000000000000 ) ;
#30269=EDGE_CURVE ( 'NONE', #77866, #88432, #108187, .T. ) ;
#30270=VECTOR ( 'NONE', #1003, 1000.000000000000227 ) ;
#30271=LINE ( 'NONE', #128861, #37671 ) ;
#30272=CARTESIAN_POINT ( 'NONE',  ( -6.183988606268994381, 28.73617430169791476, 5.000000000000000000 ) ) ;
#30273=DIRECTION ( 'NONE',  ( 0.7071067811865486830, -0.7071067811865464625, -0.000000000000000000 ) ) ;
#30274=ORIENTED_EDGE ( 'NONE', *, *, #20549, .F. ) ;
#30276=AXIS2_PLACEMENT_3D ( 'NONE', #20879, #32501, #21618 ) ;
#30277=EDGE_LOOP ( 'NONE', ( #98612, #45760, #3287, #44104, #134024 ) ) ;
#30280=LINE ( 'NONE', #87524, #8898 ) ;
#30281=VECTOR ( 'NONE', #47219, 1000.000000000000000 ) ;
#30282=ADVANCED_FACE ( 'NONE', ( #142306 ), #121231, .F. ) ;
#30283=CARTESIAN_POINT ( 'NONE',  ( 27.48921356237309155, -27.52281430457074762, 5.000000000000000000 ) ) ;
#30285=ORIENTED_EDGE ( 'NONE', *, *, #120026, .T. ) ;
#30286=VERTEX_POINT ( 'NONE', #32096 ) ;
#30287=CARTESIAN_POINT ( 'NONE',  ( -33.18398860626899705, 28.73617430169810305, 5.000000000000000000 ) ) ;
#30288=VECTOR ( 'NONE', #43171, 999.9999999999998863 ) ;
#30289=DIRECTION ( 'NONE',  ( 0.3543493200069162685, -0.000000000000000000, -0.9351131265310288487 ) ) ;
#30290=DIRECTION ( 'NONE',  ( -0.7071067811865486830, -0.7071067811865464625, 0.000000000000000000 ) ) ;
#30291=EDGE_CURVE ( 'NONE', #32044, #37569, #20478, .T. ) ;
#30292=DIRECTION ( 'NONE',  ( 0.7071067811865487940, 0.7071067811865463515, 0.000000000000000000 ) ) ;
#30293=DIRECTION ( 'NONE',  ( 1.000000000000000000, 0.000000000000000000, 0.000000000000000000 ) ) ;
#30294=VECTOR ( 'NONE', #62482, 1000.000000000000227 ) ;
#30295=VECTOR ( 'NONE', #51058, 1000.000000000000000 ) ;
#30296=CARTESIAN_POINT ( 'NONE',  ( 21.48921356237309155, -27.52281430457070499, 5.000000000000000000 ) ) ;
#30298=CARTESIAN_POINT ( 'NONE',  ( 15.18398860626900237, 28.73617430169797871, 5.000000000000000000 ) ) ;
#30300=VECTOR ( 'NONE', #121956, 1000.000000000000000 ) ;
#30301=ORIENTED_EDGE ( 'NONE', *, *, #79405, .F. ) ;
#30302=LINE ( 'NONE', #88266, #39527 ) ;
#30303=CARTESIAN_POINT ( 'NONE',  ( -1.998069433179001653, -22.22500000000000142, 4.500000000000000888 ) ) ;
#30304=AXIS2_PLACEMENT_3D ( 'NONE', #65474, #109655, #121236 ) ;
#30305=VERTEX_POINT ( 'NONE', #21923 ) ;
#30306=FACE_OUTER_BOUND ( 'NONE', #16805, .T. ) ;
#30307=CARTESIAN_POINT ( 'NONE',  ( 11.11162361894751882, 9.759292476615614831, 17.35367589129210231 ) ) ;
#30308=ORIENTED_EDGE ( 'NONE', *, *, #31646, .T. ) ;
#30309=EDGE_CURVE ( 'NONE', #2772, #89301, #9596, .T. ) ;
#30311=CARTESIAN_POINT ( 'NONE',  ( -39.29974487139159578, -27.71228299555233576, 4.000000000000000000 ) ) ;
#30312=ADVANCED_FACE ( 'NONE', ( #42990 ), #87191, .F. ) ;
#30313=CARTESIAN_POINT ( 'NONE',  ( -32.67183060077623935, 20.25929247661551358, 4.000000000000000000 ) ) ;
#30315=CARTESIAN_POINT ( 'NONE',  ( 26.67183060077628198, -15.74070752338412049, 4.000000000000000000 ) ) ;
#30316=EDGE_LOOP ( 'NONE', ( #9835, #44963, #107168, #24596 ) ) ;
#30318=ADVANCED_FACE ( 'NONE', ( #98759 ), #142995, .T. ) ;
#30322=DIRECTION ( 'NONE',  ( 0.3543493200069162685, -0.000000000000000000, -0.9351131265310288487 ) ) ;
#30324=LINE ( 'NONE', #61563, #132860 ) ;
#30325=CARTESIAN_POINT ( 'NONE',  ( -32.58838509405146056, 22.22499999999999787, 4.777194822843818578 ) ) ;
#30329=DIRECTION ( 'NONE',  ( 0.6830127018922181881, 0.6830127018922202975, -0.2588190451025214056 ) ) ;
#30330=VECTOR ( 'NONE', #92142, 1000.000000000000000 ) ;
#30331=CARTESIAN_POINT ( 'NONE',  ( -9.328169399223460445, 20.25929247661551713, 4.000000000000000000 ) ) ;
#30332=ORIENTED_EDGE ( 'NONE', *, *, #92720, .F. ) ;
#30333=EDGE_LOOP ( 'NONE', ( #66601, #40217, #134746, #92970, #58067, #43008, #20687, #23654, #99188, #78265, #37941, #127504, #43278, #38706, #67509, #90815, #103730, #75937, #138150, #24575, #22036, #55368, #12312, #87179, #24723, #60701, #130271, #40, #51909, #17582, #9423, #7730, #119512, #24430, #67627, #80583, #136633, #30516, #83471, #89120, #30054, #143307, #9524, #616, #50263, #122269, #131584, #21605, #38702, #64985, #3773, #130649, #88809, #86840, #45796, #115478, #4312, #9714, #67609, #9806, #115323, #83551, #12484, #124848, #121043, #125042, #100714, #20062, #130702, #124562, #31841, #141452, #14599, #141679, #96768, #52414, #113346, #139167, #126005, #51299, #128412, #84795, #43930, #4518, #17347, #115905 ) ) ;
#30336=CARTESIAN_POINT ( 'NONE',  ( -32.99451991528749062, 28.92564299267960948, 4.000000000000000000 ) ) ;
#30337=LINE ( 'NONE', #31771, #120286 ) ;
#30339=VECTOR ( 'NONE', #82365, 1000.000000000000000 ) ;
#30340=LINE ( 'NONE', #74580, #22400 ) ;
#30342=DIRECTION ( 'NONE',  ( 0.7071067811865486830, -0.7071067811865464625, -0.000000000000000000 ) ) ;
#30344=LINE ( 'NONE', #118772, #41955 ) ;
#30346=CARTESIAN_POINT ( 'NONE',  ( -27.28001967989386856, 0.7592924766157104211, 14.27032725228002619 ) ) ;
#30348=DIRECTION ( 'NONE',  ( -0.000000000000000000, 0.3543493200069153248, 0.9351131265310292928 ) ) ;
#30351=DIRECTION ( 'NONE',  ( 0.3543493200069163240, 0.000000000000000000, -0.9351131265310288487 ) ) ;
#30352=LINE ( 'NONE', #118780, #133603 ) ;
#30353=CARTESIAN_POINT ( 'NONE',  ( -34.82334089840005475, 5.259292476615665457, 15.86257073897106018 ) ) ;
#30354=VERTEX_POINT ( 'NONE', #135697 ) ;
#30355=ORIENTED_EDGE ( 'NONE', *, *, #106751, .F. ) ;
#30356=ORIENTED_EDGE ( 'NONE', *, *, #50898, .T. ) ;
#30358=ORIENTED_EDGE ( 'NONE', *, *, #24451, .F. ) ;
#30361=ORIENTED_EDGE ( 'NONE', *, *, #48026, .F. ) ;
#30363=DIRECTION ( 'NONE',  ( -0.000000000000000000, 0.000000000000000000, 1.000000000000000000 ) ) ;
#30364=LINE ( 'NONE', #118796, #16475 ) ;
#30365=VECTOR ( 'NONE', #59174, 1000.000000000000000 ) ;
#30366=VECTOR ( 'NONE', #33971, 1000.000000000000000 ) ;
#30369=DIRECTION ( 'NONE',  ( 0.7071067811865487940, 0.7071067811865463515, 0.000000000000000000 ) ) ;
#30370=CARTESIAN_POINT ( 'NONE',  ( 23.81601139373100295, 28.73617430169770870, 5.000000000000000000 ) ) ;
#30371=AXIS2_PLACEMENT_3D ( 'NONE', #63523, #42480, #65680 ) ;
#30373=VECTOR ( 'NONE', #62424, 1000.000000000000000 ) ;
#30375=LINE ( 'NONE', #141266, #104025 ) ;
#30377=VECTOR ( 'NONE', #111766, 1000.000000000000000 ) ;
#30378=VERTEX_POINT ( 'NONE', #45852 ) ;
#30379=ORIENTED_EDGE ( 'NONE', *, *, #69185, .T. ) ;
#30380=ORIENTED_EDGE ( 'NONE', *, *, #125426, .F. ) ;
#30381=DIRECTION ( 'NONE',  ( 0.7071067811865487940, 0.7071067811865463515, 0.000000000000000000 ) ) ;
#30382=EDGE_CURVE ( 'NONE', #131612, #135054, #111801, .T. ) ;
#30383=EDGE_CURVE ( 'NONE', #104648, #98113, #13166, .T. ) ;
#30384=LINE ( 'NONE', #63748, #61762 ) ;
#30385=VECTOR ( 'NONE', #6773, 1000.000000000000000 ) ;
#30386=CARTESIAN_POINT ( 'NONE',  ( 28.49999999999981171, 19.08746187583904330, 4.000000000000000000 ) ) ;
#30387=CARTESIAN_POINT ( 'NONE',  ( 25.22674160717818737, -11.24070752338416490, 18.24660765846988397 ) ) ;
#30388=EDGE_CURVE ( 'NONE', #88279, #5941, #68338, .T. ) ;
#30389=EDGE_CURVE ( 'NONE', #13547, #11670, #134271, .T. ) ;
#30390=ADVANCED_FACE ( 'NONE', ( #69756 ), #90028, .F. ) ;
#30391=ORIENTED_EDGE ( 'NONE', *, *, #142652, .T. ) ;
#30392=ORIENTED_EDGE ( 'NONE', *, *, #139454, .F. ) ;
#30394=CARTESIAN_POINT ( 'NONE',  ( -13.20450575203696886, 4.382956123802139281, 4.000000000000000000 ) ) ;
#30395=EDGE_CURVE ( 'NONE', #124122, #110313, #2276, .T. ) ;
#30396=EDGE_LOOP ( 'NONE', ( #1100, #102297, #75487, #115073 ) ) ;
#30397=ORIENTED_EDGE ( 'NONE', *, *, #56587, .F. ) ;
#30398=EDGE_CURVE ( 'NONE', #65672, #73773, #91484, .T. ) ;
#30399=VECTOR ( 'NONE', #73554, 1000.000000000000227 ) ;
#30400=EDGE_CURVE ( 'NONE', #15104, #127807, #78465, .T. ) ;
#30401=VECTOR ( 'NONE', #81036, 1000.000000000000000 ) ;
#30402=LINE ( 'NONE', #88916, #104470 ) ;
#30403=DIRECTION ( 'NONE',  ( -0.7071067811865487940, 0.7071067811865463515, 0.000000000000000000 ) ) ;
#30404=ORIENTED_EDGE ( 'NONE', *, *, #49724, .F. ) ;
#30405=DIRECTION ( 'NONE',  ( 0.7071067811865487940, -0.7071067811865463515, 0.000000000000000000 ) ) ;
#30407=VECTOR ( 'NONE', #55047, 1000.000000000000000 ) ;
#30408=CARTESIAN_POINT ( 'NONE',  ( -32.21837311707484020, 21.74787736706806385, 4.999607392498048419 ) ) ;
#30409=DIRECTION ( 'NONE',  ( 0.6830127018922181881, 0.6830127018922202975, -0.2588190451025214056 ) ) ;
#30411=FACE_OUTER_BOUND ( 'NONE', #123866, .T. ) ;
#30412=ORIENTED_EDGE ( 'NONE', *, *, #132692, .T. ) ;
#30413=EDGE_CURVE ( 'NONE', #123966, #84757, #13876, .T. ) ;
#30414=LINE ( 'NONE', #64463, #67328 ) ;
#30415=DIRECTION ( 'NONE',  ( -0.7071067811865486830, -0.7071067811865463515, 0.000000000000000000 ) ) ;
#30416=ORIENTED_EDGE ( 'NONE', *, *, #7527, .F. ) ;
#30418=CARTESIAN_POINT ( 'NONE',  ( 34.92499999999998295, -3.183345613589516621, 4.500000000000000888 ) ) ;
#30419=AXIS2_PLACEMENT_3D ( 'NONE', #62087, #17133, #47838 ) ;
#30420=CARTESIAN_POINT ( 'NONE',  ( -45.48921356237309510, -27.52281430457087197, 5.000000000000000000 ) ) ;
#30421=EDGE_LOOP ( 'NONE', ( #46758, #11253, #54806, #94232 ) ) ;
#30422=LINE ( 'NONE', #28994, #55149 ) ;
#30423=ORIENTED_EDGE ( 'NONE', *, *, #67938, .F. ) ;
#30424=VERTEX_POINT ( 'NONE', #22605 ) ;
#30425=ADVANCED_FACE ( 'NONE', ( #79214 ), #24079, .F. ) ;
#30428=CARTESIAN_POINT ( 'NONE',  ( -15.79289321881333841, -2.240707523384262601, 5.000000000000000000 ) ) ;
#30431=CARTESIAN_POINT ( 'NONE',  ( 34.92499999999998295, -0.1833456135895417671, 4.500000000000000888 ) ) ;
#30434=CARTESIAN_POINT ( 'NONE',  ( -30.18398860626900060, 28.73617430169808173, 5.000000000000000000 ) ) ;
#30435=VECTOR ( 'NONE', #31271, 1000.000000000000000 ) ;
#30436=LINE ( 'NONE', #97824, #52760 ) ;
#30437=LINE ( 'NONE', #50759, #97765 ) ;
#30438=CARTESIAN_POINT ( 'NONE',  ( 26.67183060077627843, -12.74070752338415069, 4.000000000000000000 ) ) ;
#30439=EDGE_CURVE ( 'NONE', #51050, #19388, #135009, .T. ) ;
#30440=DIRECTION ( 'NONE',  ( -0.7071067811865486830, 0.7071067811865464625, 0.000000000000000000 ) ) ;
#30441=CARTESIAN_POINT ( 'NONE',  ( -39.29974487139159578, -27.71228299555233576, 4.000000000000000000 ) ) ;
#30442=ORIENTED_EDGE ( 'NONE', *, *, #46463, .T. ) ;
#30443=EDGE_CURVE ( 'NONE', #42434, #48695, #58178, .T. ) ;
#30444=ORIENTED_EDGE ( 'NONE', *, *, #15363, .T. ) ;
#30446=AXIS2_PLACEMENT_3D ( 'NONE', #15278, #92144, #59565 ) ;
#30447=VERTEX_POINT ( 'NONE', #3020 ) ;
#30448=PLANE ( 'NONE',  #84268 ) ;
#30449=ORIENTED_EDGE ( 'NONE', *, *, #114762, .T. ) ;
#30450=ADVANCED_FACE ( 'NONE', ( #88633 ), #36384, .T. ) ;
#30451=ORIENTED_EDGE ( 'NONE', *, *, #71120, .F. ) ;
#30452=FACE_OUTER_BOUND ( 'NONE', #74976, .T. ) ;
#30453=LINE ( 'NONE', #96376, #29295 ) ;
#30454=DIRECTION ( 'NONE',  ( -0.000000000000000000, 0.000000000000000000, 1.000000000000000000 ) ) ;
#30455=ORIENTED_EDGE ( 'NONE', *, *, #49638, .F. ) ;
#30456=CARTESIAN_POINT ( 'NONE',  ( -42.48921356237308800, -27.52281430457085065, 5.000000000000000000 ) ) ;
#30458=ORIENTED_EDGE ( 'NONE', *, *, #54658, .F. ) ;
#30459=EDGE_CURVE ( 'NONE', #50406, #46947, #11737, .T. ) ;
#30460=DIRECTION ( 'NONE',  ( -0.6830127018922180770, -0.6830127018922204085, -0.2588190451025213501 ) ) ;
#30462=ORIENTED_EDGE ( 'NONE', *, *, #141396, .T. ) ;
#30465=CARTESIAN_POINT ( 'NONE',  ( -24.18398860626899705, 28.73617430169804265, 5.000000000000000000 ) ) ;
#30466=EDGE_CURVE ( 'NONE', #136170, #51392, #132, .T. ) ;
#30467=LINE ( 'NONE', #77561, #4848 ) ;
#30468=ORIENTED_EDGE ( 'NONE', *, *, #48772, .F. ) ;
#30469=ORIENTED_EDGE ( 'NONE', *, *, #49074, .T. ) ;
#30470=DIRECTION ( 'NONE',  ( 1.000000000000000000, 0.000000000000000000, 0.000000000000000000 ) ) ;
#30471=ORIENTED_EDGE ( 'NONE', *, *, #70739, .T. ) ;
#30473=CARTESIAN_POINT ( 'NONE',  ( -11.81601139373100651, 28.73617430169779041, 5.000000000000000000 ) ) ;
#30474=VECTOR ( 'NONE', #74355, 1000.000000000000000 ) ;
#30475=VECTOR ( 'NONE', #132284, 1000.000000000000227 ) ;
#30476=PLANE ( 'NONE',  #59029 ) ;
#30477=DIRECTION ( 'NONE',  ( 0.000000000000000000, 1.000000000000000000, 0.000000000000000000 ) ) ;
#30478=ORIENTED_EDGE ( 'NONE', *, *, #130568, .F. ) ;
#30479=AXIS2_PLACEMENT_3D ( 'NONE', #19022, #139413, #40102 ) ;
#30481=VECTOR ( 'NONE', #140930, 1000.000000000000000 ) ;
#30484=PLANE ( 'NONE',  #137140 ) ;
#30485=EDGE_LOOP ( 'NONE', ( #120391, #49834, #90834, #67399 ) ) ;
#30486=FACE_OUTER_BOUND ( 'NONE', #101849, .T. ) ;
#30489=VECTOR ( 'NONE', #70305, 1000.000000000000000 ) ;
#30491=CARTESIAN_POINT ( 'NONE',  ( -34.92500000000001137, -22.22500000000000142, 4.000000000000000000 ) ) ;
#30494=CARTESIAN_POINT ( 'NONE',  ( 33.48921356237309510, -27.52281430457078670, 5.000000000000000000 ) ) ;
#30495=VERTEX_POINT ( 'NONE', #137852 ) ;
#30496=EDGE_CURVE ( 'NONE', #77145, #65454, #17468, .T. ) ;
#30497=ORIENTED_EDGE ( 'NONE', *, *, #64943, .F. ) ;
#30498=DIRECTION ( 'NONE',  ( 0.6830127018922181881, 0.6830127018922202975, -0.2588190451025214056 ) ) ;
#30499=CARTESIAN_POINT ( 'NONE',  ( 10.49999999999992895, 6.277155672890280869, -3.510561720658966323 ) ) ;
#30500=ORIENTED_EDGE ( 'NONE', *, *, #30210, .F. ) ;
#30501=LINE ( 'NONE', #65289, #18766 ) ;
#30503=CARTESIAN_POINT ( 'NONE',  ( 14.22995720542196985, 21.73644205237998150, 5.000000000000000888 ) ) ;
#30504=ADVANCED_FACE ( 'NONE', ( #139288 ), #14623, .F. ) ;
#30505=LINE ( 'NONE', #52928, #34537 ) ;
#30506=CARTESIAN_POINT ( 'NONE',  ( 57.18398860626899705, 28.73617430169827358, 5.000000000000000000 ) ) ;
#30508=DIRECTION ( 'NONE',  ( -0.6830127018922181881, 0.6830127018922202975, -0.2588190451025214056 ) ) ;
#30509=LINE ( 'NONE', #94318, #49358 ) ;
#30510=DIRECTION ( 'NONE',  ( 1.000000000000000000, -0.000000000000000000, 0.000000000000000000 ) ) ;
#30511=LINE ( 'NONE', #75443, #87435 ) ;
#30512=CARTESIAN_POINT ( 'NONE',  ( 9.489213562373095101, -27.52281430457062328, 5.000000000000000000 ) ) ;
#30513=DIRECTION ( 'NONE',  ( 0.7071067811865487940, 0.7071067811865463515, 0.000000000000000000 ) ) ;
#30516=ORIENTED_EDGE ( 'NONE', *, *, #90259, .F. ) ;
#30517=EDGE_CURVE ( 'NONE', #94326, #7871, #84199, .T. ) ;
#30519=ORIENTED_EDGE ( 'NONE', *, *, #94457, .T. ) ;
#30520=ORIENTED_EDGE ( 'NONE', *, *, #127956, .F. ) ;
#30522=VECTOR ( 'NONE', #94557, 1000.000000000000227 ) ;
#30523=ADVANCED_FACE ( 'NONE', ( #105883 ), #92891, .F. ) ;
#30524=ORIENTED_EDGE ( 'NONE', *, *, #113442, .T. ) ;
#30525=ORIENTED_EDGE ( 'NONE', *, *, #25432, .F. ) ;
#30526=AXIS2_PLACEMENT_3D ( 'NONE', #132821, #46542, #111002 ) ;
#30528=CARTESIAN_POINT ( 'NONE',  ( -62.99451991528749772, 28.92564299267982264, 4.000000000000000000 ) ) ;
#30530=AXIS2_PLACEMENT_3D ( 'NONE', #86357, #129123, #130576 ) ;
#30531=EDGE_LOOP ( 'NONE', ( #28979, #127911, #131746, #31189 ) ) ;
#30532=LINE ( 'NONE', #21783, #23132 ) ;
#30533=CARTESIAN_POINT ( 'NONE',  ( -19.64175702458847894, 15.75929247661555088, 19.34181609438704186 ) ) ;
#30534=CARTESIAN_POINT ( 'NONE',  ( 3.060110710440185233, -9.740707523384184441, 10.89222023123380190 ) ) ;
#30536=ORIENTED_EDGE ( 'NONE', *, *, #111769, .T. ) ;
#30537=EDGE_CURVE ( 'NONE', #138203, #11420, #92164, .T. ) ;
#30538=CARTESIAN_POINT ( 'NONE',  ( -39.48921356237310221, -27.52281430457082934, 5.000000000000000000 ) ) ;
#30540=LINE ( 'NONE', #44284, #117016 ) ;
#30541=VECTOR ( 'NONE', #59006, 1000.000000000000000 ) ;
#30542=DIRECTION ( 'NONE',  ( 0.7071067811865487940, 0.7071067811865463515, 0.000000000000000000 ) ) ;
#30543=DIRECTION ( 'NONE',  ( -0.7071067811865486830, -0.7071067811865464625, 0.000000000000000000 ) ) ;
#30545=FACE_OUTER_BOUND ( 'NONE', #43147, .T. ) ;
#30547=ORIENTED_EDGE ( 'NONE', *, *, #116657, .T. ) ;
#30549=ORIENTED_EDGE ( 'NONE', *, *, #142147, .F. ) ;
#30552=LINE ( 'NONE', #21805, #38631 ) ;
#30554=AXIS2_PLACEMENT_3D ( 'NONE', #52244, #8003, #118923 ) ;
#30555=CARTESIAN_POINT ( 'NONE',  ( 20.81601139373100295, 28.73617430169773002, 5.000000000000000000 ) ) ;
#30558=CARTESIAN_POINT ( 'NONE',  ( 26.99999999999981526, 1.761378380278708855, -6.096875308897192980 ) ) ;
#30560=ORIENTED_EDGE ( 'NONE', *, *, #76104, .T. ) ;
#30561=LINE ( 'NONE', #62474, #138250 ) ;
#30562=EDGE_CURVE ( 'NONE', #98330, #137557, #93621, .T. ) ;
#30566=CARTESIAN_POINT ( 'NONE',  ( -57.18398860626899705, 28.73617430169827358, 5.000000000000000000 ) ) ;
#30567=CARTESIAN_POINT ( 'NONE',  ( -33.52400138585426248, 22.03583458319438648, 4.979811245910084061 ) ) ;
#30569=DIRECTION ( 'NONE',  ( -0.7071067811865486830, -0.7071067811865464625, 0.000000000000000000 ) ) ;
#30570=ORIENTED_EDGE ( 'NONE', *, *, #21397, .F. ) ;
#30572=EDGE_LOOP ( 'NONE', ( #142808, #27349, #88938, #107415 ) ) ;
#30573=FACE_OUTER_BOUND ( 'NONE', #62930, .T. ) ;
#30574=DIRECTION ( 'NONE',  ( -0.3543493200069162685, -0.000000000000000000, -0.9351131265310288487 ) ) ;
#30575=FACE_OUTER_BOUND ( 'NONE', #53674, .T. ) ;
#30576=LINE ( 'NONE', #127002, #117877 ) ;
#30578=EDGE_CURVE ( 'NONE', #103011, #83238, #5134, .T. ) ;
#30580=EDGE_CURVE ( 'NONE', #32788, #13363, #128394, .T. ) ;
#30581=ORIENTED_EDGE ( 'NONE', *, *, #48898, .F. ) ;
#30582=CARTESIAN_POINT ( 'NONE',  ( -5.510786437626906675, -27.52281430457051314, 5.000000000000000000 ) ) ;
#30583=EDGE_CURVE ( 'NONE', #39610, #71573, #125543, .T. ) ;
#30584=ORIENTED_EDGE ( 'NONE', *, *, #106011, .F. ) ;
#30588=ORIENTED_EDGE ( 'NONE', *, *, #96211, .T. ) ;
#30589=VECTOR ( 'NONE', #46476, 1000.000000000000000 ) ;
#30590=EDGE_CURVE ( 'NONE', #79833, #121192, #126247, .T. ) ;
#30593=CARTESIAN_POINT ( 'NONE',  ( -2.999999999999981792, 4.384688058510565867, -7.090945410444692953 ) ) ;
#30595=CARTESIAN_POINT ( 'NONE',  ( -34.47516574401892342, 6.028067341115762368, 4.998110765256835286 ) ) ;
#30596=EDGE_CURVE ( 'NONE', #104186, #86287, #47994, .T. ) ;
#30598=VECTOR ( 'NONE', #84551, 999.9999999999998863 ) ;
#30600=LINE ( 'NONE', #42905, #106100 ) ;
#30601=LINE ( 'NONE', #8079, #14141 ) ;
#30603=FACE_BOUND ( 'NONE', #52370, .T. ) ;
#30604=ORIENTED_EDGE ( 'NONE', *, *, #72724, .F. ) ;
#30605=EDGE_CURVE ( 'NONE', #49793, #108166, #103067, .T. ) ;
#30606=PLANE ( 'NONE',  #71166 ) ;
#30609=VERTEX_POINT ( 'NONE', #136393 ) ;
#30610=LINE ( 'NONE', #74838, #73562 ) ;
#30611=EDGE_LOOP ( 'NONE', ( #105141, #39756, #3899, #42420 ) ) ;
#30612=VERTEX_POINT ( 'NONE', #16011 ) ;
#30613=DIRECTION ( 'NONE',  ( 0.7071067811865486830, -0.7071067811865464625, -0.000000000000000000 ) ) ;
#30614=ADVANCED_FACE ( 'NONE', ( #71891 ), #3700, .F. ) ;
#30615=EDGE_LOOP ( 'NONE', ( #24656, #64141, #116118, #26932, #116258 ) ) ;
#30617=ORIENTED_EDGE ( 'NONE', *, *, #20192, .F. ) ;
#30618=CARTESIAN_POINT ( 'NONE',  ( 0.000000000000000000, 0.000000000000000000, 5.000000000000000000 ) ) ;
#30619=LINE ( 'NONE', #116179, #7881 ) ;
#30620=ORIENTED_EDGE ( 'NONE', *, *, #44494, .T. ) ;
#30621=DIRECTION ( 'NONE',  ( 0.7071067811865487940, 0.7071067811865463515, 0.000000000000000000 ) ) ;
#30622=PLANE ( 'NONE',  #4082 ) ;
#30623=VECTOR ( 'NONE', #129530, 1000.000000000000000 ) ;
#30624=VECTOR ( 'NONE', #16850, 1000.000000000000227 ) ;
#30626=CARTESIAN_POINT ( 'NONE',  ( 18.81246187583933960, -22.22500000000000142, 4.000000000000000000 ) ) ;
#30627=LINE ( 'NONE', #119034, #11108 ) ;
#30628=VECTOR ( 'NONE', #10109, 1000.000000000000227 ) ;
#30629=LINE ( 'NONE', #97246, #84004 ) ;
#30630=LINE ( 'NONE', #19017, #20944 ) ;
#30631=ORIENTED_EDGE ( 'NONE', *, *, #101805, .F. ) ;
#30633=ORIENTED_EDGE ( 'NONE', *, *, #7110, .F. ) ;
#30634=VECTOR ( 'NONE', #17333, 1000.000000000000000 ) ;
#30635=CARTESIAN_POINT ( 'NONE',  ( 0.000000000000000000, 0.000000000000000000, 5.000000000000000000 ) ) ;
#30636=LINE ( 'NONE', #61161, #324 ) ;
#30637=ORIENTED_EDGE ( 'NONE', *, *, #9673, .T. ) ;
#30638=EDGE_LOOP ( 'NONE', ( #63307, #125669, #48548, #22363 ) ) ;
#30639=ORIENTED_EDGE ( 'NONE', *, *, #139427, .T. ) ;
#30640=CARTESIAN_POINT ( 'NONE',  ( -26.48334561358936412, 22.22500000000000142, 4.500000000000000888 ) ) ;
#30641=FACE_OUTER_BOUND ( 'NONE', #127278, .T. ) ;
#30642=DIRECTION ( 'NONE',  ( 0.7071067811865486830, -0.7071067811865464625, -0.000000000000000000 ) ) ;
#30643=ORIENTED_EDGE ( 'NONE', *, *, #108072, .T. ) ;
#30646=CARTESIAN_POINT ( 'NONE',  ( -24.48921356237309510, -27.52281430457072631, 5.000000000000000000 ) ) ;
#30648=ORIENTED_EDGE ( 'NONE', *, *, #46026, .F. ) ;
#30651=ADVANCED_FACE ( 'NONE', ( #18895 ), #42110, .F. ) ;
#30652=AXIS2_PLACEMENT_3D ( 'NONE', #93853, #140229, #16252 ) ;
#30653=CARTESIAN_POINT ( 'NONE',  ( 0.000000000000000000, 0.000000000000000000, 5.000000000000000000 ) ) ;
#30655=ORIENTED_EDGE ( 'NONE', *, *, #26284, .T. ) ;
#30656=DIRECTION ( 'NONE',  ( -0.000000000000000000, 0.000000000000000000, 1.000000000000000000 ) ) ;
#30657=VECTOR ( 'NONE', #35535, 1000.000000000000000 ) ;
#30659=LINE ( 'NONE', #53842, #91290 ) ;
#30660=LINE ( 'NONE', #72774, #35468 ) ;
#30662=VERTEX_POINT ( 'NONE', #84874 ) ;
#30663=ADVANCED_FACE ( 'NONE', ( #54422 ), #9411, .F. ) ;
#30666=VECTOR ( 'NONE', #116037, 1000.000000000000000 ) ;
#30667=EDGE_LOOP ( 'NONE', ( #58525, #43132, #92873, #44340, #125708 ) ) ;
#30668=VECTOR ( 'NONE', #55353, 1000.000000000000000 ) ;
#30669=CARTESIAN_POINT ( 'NONE',  ( -2.510786437626908008, -27.52281430457053446, 5.000000000000000000 ) ) ;
#30670=CARTESIAN_POINT ( 'NONE',  ( -6.299744871391586898, -27.71228299555210484, 4.000000000000000000 ) ) ;
#30672=CARTESIAN_POINT ( 'NONE',  ( 34.42499999999998295, 0.000000000000000000, 4.500000000000000888 ) ) ;
#30673=LINE ( 'NONE', #63321, #4388 ) ;
#30674=ORIENTED_EDGE ( 'NONE', *, *, #131131, .F. ) ;
#30675=EDGE_CURVE ( 'NONE', #102238, #85157, #7286, .T. ) ;
#30676=ORIENTED_EDGE ( 'NONE', *, *, #57465, .F. ) ;
#30677=VECTOR ( 'NONE', #90808, 999.9999999999998863 ) ;
#30678=LINE ( 'NONE', #85737, #40268 ) ;
#30679=LINE ( 'NONE', #65460, #11224 ) ;
#30681=DIRECTION ( 'NONE',  ( -0.000000000000000000, -0.000000000000000000, 1.000000000000000000 ) ) ;
#30682=PLANE ( 'NONE',  #43751 ) ;
#30683=LINE ( 'NONE', #119090, #100014 ) ;
#30684=ORIENTED_EDGE ( 'NONE', *, *, #92398, .T. ) ;
#30686=LINE ( 'NONE', #32834, #5031 ) ;
#30687=CARTESIAN_POINT ( 'NONE',  ( 72.18398860626899705, 28.73617430169837661, 5.000000000000000000 ) ) ;
#30688=AXIS2_PLACEMENT_3D ( 'NONE', #34240, #110334, #78462 ) ;
#30689=VECTOR ( 'NONE', #60459, 1000.000000000000227 ) ;
#30691=DIRECTION ( 'NONE',  ( 0.7071067811865487940, 0.7071067811865463515, -0.000000000000000000 ) ) ;
#30693=CARTESIAN_POINT ( 'NONE',  ( 25.49999999999982592, -2.947814304570800736, 5.000000000000000000 ) ) ;
#30694=AXIS2_PLACEMENT_3D ( 'NONE', #78068, #22915, #1176 ) ;
#30695=AXIS2_PLACEMENT_3D ( 'NONE', #59500, #49350, #58821 ) ;
#30696=ORIENTED_EDGE ( 'NONE', *, *, #68411, .F. ) ;
#30697=CARTESIAN_POINT ( 'NONE',  ( -10.49999999999992006, 18.05218569542898521, 5.000000000000000000 ) ) ;
#30698=EDGE_CURVE ( 'NONE', #85690, #22619, #41356, .T. ) ;
#30699=ORIENTED_EDGE ( 'NONE', *, *, #93774, .F. ) ;
#30700=ADVANCED_FACE ( 'NONE', ( #95747 ), #21029, .F. ) ;
#30701=VERTEX_POINT ( 'NONE', #20307 ) ;
#30702=AXIS2_PLACEMENT_3D ( 'NONE', #102399, #82775, #59610 ) ;
#30703=LINE ( 'NONE', #43000, #66385 ) ;
#30704=( GEOMETRIC_REPRESENTATION_CONTEXT ( 3 ) GLOBAL_UNCERTAINTY_ASSIGNED_CONTEXT ( ( #140315 ) ) GLOBAL_UNIT_ASSIGNED_CONTEXT ( ( #121660, #109372, #98496 ) ) REPRESENTATION_CONTEXT ( 'NONE', 'WORKASPACE' ) );
#30705=DIRECTION ( 'NONE',  ( 0.7071067811865487940, -0.7071067811865463515, 0.000000000000000000 ) ) ;
#30706=VERTEX_POINT ( 'NONE', #142137 ) ;
#30707=PLANE ( 'NONE',  #29989 ) ;
#30708=LINE ( 'NONE', #8860, #127548 ) ;
#30709=CARTESIAN_POINT ( 'NONE',  ( -6.183988606268994381, 28.73617430169791476, 5.000000000000000000 ) ) ;
#30710=EDGE_CURVE ( 'NONE', #57071, #115637, #108730, .T. ) ;
#30711=DIRECTION ( 'NONE',  ( -0.7071067811865486830, -0.7071067811865464625, 0.000000000000000000 ) ) ;
#30714=ADVANCED_FACE ( 'NONE', ( #109483 ), #75439, .F. ) ;
#30715=CARTESIAN_POINT ( 'NONE',  ( -34.92500000000001137, 7.800094516027127334, 4.759050581649336920 ) ) ;
#30716=FACE_OUTER_BOUND ( 'NONE', #14335, .T. ) ;
#30717=DIRECTION ( 'NONE',  ( -0.7071067811865486830, -0.7071067811865464625, 0.000000000000000000 ) ) ;
#30718=DIRECTION ( 'NONE',  ( -0.7071067811865487940, 0.7071067811865463515, -0.000000000000000000 ) ) ;
#30719=FACE_OUTER_BOUND ( 'NONE', #47089, .T. ) ;
#30720=CARTESIAN_POINT ( 'NONE',  ( -11.29289321881337571, 11.25929247661560240, 5.000000000000000000 ) ) ;
#30722=VECTOR ( 'NONE', #86666, 1000.000000000000000 ) ;
#30723=DIRECTION ( 'NONE',  ( 0.7071067811865487940, -0.7071067811865463515, 0.000000000000000000 ) ) ;
#30724=ORIENTED_EDGE ( 'NONE', *, *, #118909, .F. ) ;
#30725=EDGE_LOOP ( 'NONE', ( #110577, #291, #91112, #100513 ) ) ;
#30728=LINE ( 'NONE', #42320, #134229 ) ;
#30729=DIRECTION ( 'NONE',  ( -0.6830127018922180770, -0.6830127018922204085, -0.2588190451025213501 ) ) ;
#30730=VERTEX_POINT ( 'NONE', #10160 ) ;
#30732=DIRECTION ( 'NONE',  ( 1.000000000000000000, 0.000000000000000000, 0.000000000000000000 ) ) ;
#30734=VECTOR ( 'NONE', #118701, 1000.000000000000227 ) ;
#30735=ORIENTED_EDGE ( 'NONE', *, *, #49253, .T. ) ;
#30736=LINE ( 'NONE', #95245, #110381 ) ;
#30737=EDGE_LOOP ( 'NONE', ( #124482, #29239, #8505, #80392 ) ) ;
#30738=ORIENTED_EDGE ( 'NONE', *, *, #16234, .F. ) ;
#30739=CIRCLE ( 'NONE', #63139, 0.5000000000000004441 ) ;
#30742=DIRECTION ( 'NONE',  ( -0.7071067811865486830, -0.7071067811865464625, -0.000000000000000000 ) ) ;
#30743=CARTESIAN_POINT ( 'NONE',  ( 53.99451991528749062, 28.92564299267975869, 4.000000000000000000 ) ) ;
#30745=CARTESIAN_POINT ( 'NONE',  ( -23.27718569542924243, -21.72500000000000142, 5.000000000000000000 ) ) ;
#30746=DIRECTION ( 'NONE',  ( -0.7071067811865486830, 0.7071067811865464625, 0.000000000000000000 ) ) ;
#30748=ORIENTED_EDGE ( 'NONE', *, *, #143065, .F. ) ;
#30751=PLANE ( 'NONE',  #50079 ) ;
#30753=EDGE_CURVE ( 'NONE', #89800, #75311, #40670, .T. ) ;
#30754=ORIENTED_EDGE ( 'NONE', *, *, #24203, .F. ) ;
#30756=EDGE_CURVE ( 'NONE', #8995, #85957, #129083, .T. ) ;
#30757=DIRECTION ( 'NONE',  ( -0.000000000000000000, 0.000000000000000000, 1.000000000000000000 ) ) ;
#30758=VECTOR ( 'NONE', #38601, 1000.000000000000000 ) ;
#30759=DIRECTION ( 'NONE',  ( 0.7071067811865486830, -0.7071067811865464625, -0.000000000000000000 ) ) ;
#30760=DIRECTION ( 'NONE',  ( -0.7071067811865486830, -0.7071067811865464625, 0.000000000000000000 ) ) ;
#30761=EDGE_LOOP ( 'NONE', ( #110782, #56873, #1665, #61034 ) ) ;
#30763=AXIS2_PLACEMENT_3D ( 'NONE', #75821, #66375, #133764 ) ;
#30764=DIRECTION ( 'NONE',  ( -0.7071067811865486830, 0.7071067811865464625, 0.000000000000000000 ) ) ;
#30765=VERTEX_POINT ( 'NONE', #65296 ) ;
#30766=EDGE_CURVE ( 'NONE', #92260, #57761, #131968, .T. ) ;
#30768=VERTEX_POINT ( 'NONE', #73304 ) ;
#30769=PLANE ( 'NONE',  #9691 ) ;
#30770=ORIENTED_EDGE ( 'NONE', *, *, #96517, .F. ) ;
#30771=DIRECTION ( 'NONE',  ( -0.7071067811865486830, -0.7071067811865464625, 0.000000000000000000 ) ) ;
#30772=CARTESIAN_POINT ( 'NONE',  ( 34.92499999999998295, 11.57121408575943633, 9.037117742336738146 ) ) ;
#30773=VECTOR ( 'NONE', #2734, 1000.000000000000000 ) ;
#30774=CARTESIAN_POINT ( 'NONE',  ( 12.18398860626900060, 28.73617430169795739, 5.000000000000000000 ) ) ;
#30775=EDGE_CURVE ( 'NONE', #47321, #51992, #117474, .T. ) ;
#30776=FACE_BOUND ( 'NONE', #33476, .T. ) ;
#30777=EDGE_CURVE ( 'NONE', #105009, #94334, #87021, .T. ) ;
#30779=DIRECTION ( 'NONE',  ( 0.3543493200069162685, -0.000000000000000000, -0.9351131265310288487 ) ) ;
#30780=AXIS2_PLACEMENT_3D ( 'NONE', #71741, #6400, #7864 ) ;
#30781=FACE_OUTER_BOUND ( 'NONE', #28859, .T. ) ;
#30782=DIRECTION ( 'NONE',  ( -0.000000000000000000, 0.3543493200069153248, 0.9351131265310292928 ) ) ;
#30783=VERTEX_POINT ( 'NONE', #31926 ) ;
#30784=EDGE_CURVE ( 'NONE', #106288, #75799, #2849, .T. ) ;
#30785=ORIENTED_EDGE ( 'NONE', *, *, #69741, .F. ) ;
#30786=EDGE_LOOP ( 'NONE', ( #54811, #121210, #17896, #67181 ) ) ;
#30789=CARTESIAN_POINT ( 'NONE',  ( -69.48921356237309510, -27.52281430457103895, 5.000000000000000000 ) ) ;
#30792=EDGE_CURVE ( 'NONE', #41256, #139718, #55841, .T. ) ;
#30793=VECTOR ( 'NONE', #57421, 1000.000000000000000 ) ;
#30794=VECTOR ( 'NONE', #32068, 1000.000000000000000 ) ;
#30795=AXIS2_PLACEMENT_3D ( 'NONE', #93728, #70591, #82170 ) ;
#30796=DIRECTION ( 'NONE',  ( -0.000000000000000000, 0.3543493200069153248, 0.9351131265310292928 ) ) ;
#30797=LINE ( 'NONE', #66983, #134082 ) ;
#30798=CARTESIAN_POINT ( 'NONE',  ( -10.49999999999992184, -13.53360074219759746, 5.000000000000000000 ) ) ;
#30799=LINE ( 'NONE', #32955, #94413 ) ;
#30800=CARTESIAN_POINT ( 'NONE',  ( 16.49999999999988987, -10.53360074219763121, 5.000000000000000000 ) ) ;
#30801=DIRECTION ( 'NONE',  ( -0.7071067811865486830, -0.7071067811865464625, 0.000000000000000000 ) ) ;
#30802=CARTESIAN_POINT ( 'NONE',  ( 12.29974487139158512, -27.71228299555214747, 4.000000000000000000 ) ) ;
#30803=ORIENTED_EDGE ( 'NONE', *, *, #38592, .F. ) ;
#30804=VECTOR ( 'NONE', #82187, 1000.000000000000227 ) ;
#30805=ADVANCED_FACE ( 'NONE', ( #89859 ), #57999, .F. ) ;
#30806=AXIS2_PLACEMENT_3D ( 'NONE', #34628, #3395, #122317 ) ;
#30807=CARTESIAN_POINT ( 'NONE',  ( 26.67183060077628198, -6.740707523384212863, 4.000000000000000000 ) ) ;
#30808=ORIENTED_EDGE ( 'NONE', *, *, #104179, .T. ) ;
#30809=CARTESIAN_POINT ( 'NONE',  ( 5.999999999999960032, -4.447814304570786526, 5.000000000000000000 ) ) ;
#30810=CARTESIAN_POINT ( 'NONE',  ( 45.18398860626900415, 28.73617430169818832, 5.000000000000000000 ) ) ;
#30812=ORIENTED_EDGE ( 'NONE', *, *, #92233, .T. ) ;
#30813=ORIENTED_EDGE ( 'NONE', *, *, #88857, .F. ) ;
#30816=EDGE_CURVE ( 'NONE', #140054, #31371, #110176, .T. ) ;
#30817=VECTOR ( 'NONE', #65329, 1000.000000000000000 ) ;
#30819=CARTESIAN_POINT ( 'NONE',  ( 22.49999999999984368, -19.91253812416055169, 4.000000000000000000 ) ) ;
#30820=EDGE_CURVE ( 'NONE', #86975, #102218, #99290, .T. ) ;
#30821=AXIS2_PLACEMENT_3D ( 'NONE', #62431, #108731, #52933 ) ;
#30824=ORIENTED_EDGE ( 'NONE', *, *, #134853, .T. ) ;
#30825=CARTESIAN_POINT ( 'NONE',  ( -18.70710678118640402, -9.740707523384182664, 5.000000000000000000 ) ) ;
#30826=ORIENTED_EDGE ( 'NONE', *, *, #35186, .T. ) ;
#30827=CARTESIAN_POINT ( 'NONE',  ( 2.878526836628512164, -20.24070752338406720, 7.412974875817785581 ) ) ;
#30828=CARTESIAN_POINT ( 'NONE',  ( -21.48921356237309155, -27.52281430457070499, 5.000000000000000000 ) ) ;
#30829=CARTESIAN_POINT ( 'NONE',  ( 34.47516574401891631, 18.02806734111562292, 4.998110765256834398 ) ) ;
#30830=VERTEX_POINT ( 'NONE', #34085 ) ;
#30831=ORIENTED_EDGE ( 'NONE', *, *, #133584, .F. ) ;
#30834=LINE ( 'NONE', #55428, #130481 ) ;
#30835=ORIENTED_EDGE ( 'NONE', *, *, #129795, .T. ) ;
#30836=DIRECTION ( 'NONE',  ( -0.7071067811865486830, -0.7071067811865464625, 0.000000000000000000 ) ) ;
#30837=ORIENTED_EDGE ( 'NONE', *, *, #59729, .T. ) ;
#30838=VERTEX_POINT ( 'NONE', #1403 ) ;
#30839=VECTOR ( 'NONE', #58343, 1000.000000000000000 ) ;
#30840=VERTEX_POINT ( 'NONE', #77596 ) ;
#30841=FACE_OUTER_BOUND ( 'NONE', #131458, .T. ) ;
#30843=FACE_OUTER_BOUND ( 'NONE', #103134, .T. ) ;
#30844=CARTESIAN_POINT ( 'NONE',  ( 19.49999999999986855, 22.01701374228156993, 2.453858888625586321 ) ) ;
#30845=CARTESIAN_POINT ( 'NONE',  ( -24.32816939922335919, -18.74070752338409207, 4.000000000000000000 ) ) ;
#30847=EDGE_LOOP ( 'NONE', ( #87110, #16425, #59019, #35641 ) ) ;
#30848=EDGE_CURVE ( 'NONE', #38978, #116079, #24608, .T. ) ;
#30850=ORIENTED_EDGE ( 'NONE', *, *, #64758, .T. ) ;
#30851=LINE ( 'NONE', #75080, #100385 ) ;
#30854=VECTOR ( 'NONE', #18486, 1000.000000000000227 ) ;
#30855=ORIENTED_EDGE ( 'NONE', *, *, #43677, .F. ) ;
#30856=DIRECTION ( 'NONE',  ( 0.7071067811865487940, 0.7071067811865463515, -0.000000000000000000 ) ) ;
#30857=DIRECTION ( 'NONE',  ( -0.000000000000000000, 0.000000000000000000, 1.000000000000000000 ) ) ;
#30859=VERTEX_POINT ( 'NONE', #134104 ) ;
#30860=ADVANCED_FACE ( 'NONE', ( #133396 ), #32652, .F. ) ;
#30861=DIRECTION ( 'NONE',  ( 0.3543493200069162685, -0.000000000000000000, -0.9351131265310288487 ) ) ;
#30862=CARTESIAN_POINT ( 'NONE',  ( 8.999999999999937828, -21.41253812416053748, 4.000000000000000000 ) ) ;
#30863=DIRECTION ( 'NONE',  ( -0.000000000000000000, 0.000000000000000000, 1.000000000000000000 ) ) ;
#30864=VECTOR ( 'NONE', #27844, 1000.000000000000227 ) ;
#30865=LINE ( 'NONE', #63507, #89084 ) ;
#30867=LINE ( 'NONE', #95380, #11642 ) ;
#30868=LINE ( 'NONE', #51184, #4695 ) ;
#30869=DIRECTION ( 'NONE',  ( 0.3543493200069162685, -0.000000000000000000, -0.9351131265310288487 ) ) ;
#30870=ORIENTED_EDGE ( 'NONE', *, *, #129401, .T. ) ;
#30871=CARTESIAN_POINT ( 'NONE',  ( 24.70710678118637205, -18.74070752338408852, 5.000000000000000000 ) ) ;
#30872=ORIENTED_EDGE ( 'NONE', *, *, #65201, .F. ) ;
#30873=AXIS2_PLACEMENT_3D ( 'NONE', #93213, #72232, #129398 ) ;
#30874=PLANE ( 'NONE',  #138089 ) ;
#30876=ORIENTED_EDGE ( 'NONE', *, *, #29135, .F. ) ;
#30877=PLANE ( 'NONE',  #41381 ) ;
#30878=DIRECTION ( 'NONE',  ( 0.7071067811865486830, -0.7071067811865464625, -0.000000000000000000 ) ) ;
#30879=ORIENTED_EDGE ( 'NONE', *, *, #139111, .T. ) ;
#30880=LINE ( 'NONE', #70996, #71752 ) ;
#30881=ADVANCED_FACE ( 'NONE', ( #123949 ), #79767, .F. ) ;
#30882=DIRECTION ( 'NONE',  ( -0.6830127018922180770, -0.6830127018922204085, -0.2588190451025213501 ) ) ;
#30883=PLANE ( 'NONE',  #103229 ) ;
#30884=ORIENTED_EDGE ( 'NONE', *, *, #79615, .F. ) ;
#30885=EDGE_CURVE ( 'NONE', #16391, #63562, #122480, .T. ) ;
#30886=AXIS2_PLACEMENT_3D ( 'NONE', #100445, #68549, #3246 ) ;
#30887=ORIENTED_EDGE ( 'NONE', *, *, #50871, .T. ) ;
#30888=DIRECTION ( 'NONE',  ( -0.000000000000000000, -0.3543493200069152693, 0.9351131265310292928 ) ) ;
#30889=LINE ( 'NONE', #53318, #25932 ) ;
#30891=CARTESIAN_POINT ( 'NONE',  ( -54.18398860626899705, 28.73617430169825226, 5.000000000000000000 ) ) ;
#30892=CARTESIAN_POINT ( 'NONE',  ( -5.999999999999956479, -13.06887692260767508, 4.000000000000000000 ) ) ;
#30894=ADVANCED_FACE ( 'NONE', ( #111631 ), #123240, .F. ) ;
#30895=PLANE ( 'NONE',  #37698 ) ;
#30896=DIRECTION ( 'NONE',  ( 0.7071067811865487940, 0.7071067811865463515, 0.000000000000000000 ) ) ;
#30899=VERTEX_POINT ( 'NONE', #78295 ) ;
#30900=EDGE_CURVE ( 'NONE', #8157, #24024, #45689, .T. ) ;
#30901=VECTOR ( 'NONE', #95857, 1000.000000000000227 ) ;
#30902=CARTESIAN_POINT ( 'NONE',  ( -72.48921356237309510, -27.52281430457106026, 5.000000000000000000 ) ) ;
#30903=EDGE_LOOP ( 'NONE', ( #116344, #80020, #85796, #74555 ) ) ;
#30905=LINE ( 'NONE', #107006, #84778 ) ;
#30906=VECTOR ( 'NONE', #45212, 1000.000000000000227 ) ;
#30907=CARTESIAN_POINT ( 'NONE',  ( 45.48921356237309510, -27.52281430457087197, 5.000000000000000000 ) ) ;
#30908=ORIENTED_EDGE ( 'NONE', *, *, #57740, .F. ) ;
#30909=EDGE_CURVE ( 'NONE', #130020, #91987, #143536, .T. ) ;
#30910=CARTESIAN_POINT ( 'NONE',  ( -11.51078643762690490, -27.52281430457047406, 5.000000000000000000 ) ) ;
#30911=DIRECTION ( 'NONE',  ( -0.7071067811865487940, -0.7071067811865463515, -0.000000000000000000 ) ) ;
#30912=CARTESIAN_POINT ( 'NONE',  ( -53.99451991528749062, 28.92564299267975869, 4.000000000000000000 ) ) ;
#30913=CARTESIAN_POINT ( 'NONE',  ( 0.000000000000000000, 0.000000000000000000, 5.000000000000000000 ) ) ;
#30914=DIRECTION ( 'NONE',  ( -0.7071067811865486830, -0.7071067811865464625, 0.000000000000000000 ) ) ;
#30915=ORIENTED_EDGE ( 'NONE', *, *, #88710, .T. ) ;
#30916=DIRECTION ( 'NONE',  ( -0.7071067811865486830, -0.7071067811865464625, 0.000000000000000000 ) ) ;
#30917=CARTESIAN_POINT ( 'NONE',  ( -10.49999999999992362, -17.91344420646043289, 1.358650452708439538 ) ) ;
#30918=DIRECTION ( 'NONE',  ( -0.7071067811865486830, -0.7071067811865464625, 0.000000000000000000 ) ) ;
#30921=VERTEX_POINT ( 'NONE', #2101 ) ;
#30922=EDGE_LOOP ( 'NONE', ( #33891, #27227, #111118, #131288 ) ) ;
#30924=AXIS2_PLACEMENT_3D ( 'NONE', #116787, #139998, #17469 ) ;
#30925=VERTEX_POINT ( 'NONE', #68863 ) ;
#30927=EDGE_CURVE ( 'NONE', #119366, #116312, #132705, .T. ) ;
#30928=DIRECTION ( 'NONE',  ( 0.3543493200069162685, -0.000000000000000000, -0.9351131265310288487 ) ) ;
#30929=LINE ( 'NONE', #119323, #98895 ) ;
#30930=CARTESIAN_POINT ( 'NONE',  ( -42.18398860626899705, 28.73617430169816700, 5.000000000000000000 ) ) ;
#30932=LINE ( 'NONE', #20013, #88603 ) ;
#30933=CARTESIAN_POINT ( 'NONE',  ( 35.99451991528749772, 28.92564299267963079, 4.000000000000000000 ) ) ;
#30934=VECTOR ( 'NONE', #79357, 1000.000000000000227 ) ;
#30935=ADVANCED_FACE ( 'NONE', ( #23915 ), #68176, .T. ) ;
#30936=ADVANCED_FACE ( 'NONE', ( #101453 ), #26752, .T. ) ;
#30937=VERTEX_POINT ( 'NONE', #83282 ) ;
#30939=FACE_OUTER_BOUND ( 'NONE', #87273, .T. ) ;
#30941=CARTESIAN_POINT ( 'NONE',  ( 42.18398860626899705, 28.73617430169816700, 5.000000000000000000 ) ) ;
#30942=EDGE_CURVE ( 'NONE', #41501, #105119, #94136, .T. ) ;
#30943=VERTEX_POINT ( 'NONE', #36907 ) ;
#30944=VECTOR ( 'NONE', #138886, 1000.000000000000000 ) ;
#30945=ORIENTED_EDGE ( 'NONE', *, *, #48524, .F. ) ;
#30946=EDGE_CURVE ( 'NONE', #20788, #112121, #105711, .T. ) ;
#30947=FACE_BOUND ( 'NONE', #72021, .T. ) ;
#30948=EDGE_CURVE ( 'NONE', #78047, #59514, #49955, .T. ) ;
#30949=CARTESIAN_POINT ( 'NONE',  ( -24.31657961132774304, -6.740707523384216415, 11.88629033278130009 ) ) ;
#30950=LINE ( 'NONE', #31649, #42085 ) ;
#30953=VECTOR ( 'NONE', #97610, 1000.000000000000000 ) ;
#30954=LINE ( 'NONE', #120036, #113723 ) ;
#30955=EDGE_LOOP ( 'NONE', ( #103017, #111021, #41742 ) ) ;
#30956=ADVANCED_FACE ( 'NONE', ( #114463 ), #92710, .F. ) ;
#30958=VERTEX_POINT ( 'NONE', #50647 ) ;
#30959=ORIENTED_EDGE ( 'NONE', *, *, #34919, .F. ) ;
#30960=EDGE_CURVE ( 'NONE', #45624, #28995, #38354, .T. ) ;
#30961=EDGE_LOOP ( 'NONE', ( #60954, #15373, #65312, #124943 ) ) ;
#30962=VECTOR ( 'NONE', #133256, 1000.000000000000000 ) ;
#30964=EDGE_CURVE ( 'NONE', #89868, #114456, #72449, .T. ) ;
#30966=DIRECTION ( 'NONE',  ( -0.6830127018922180770, -0.6830127018922204085, -0.2588190451025213501 ) ) ;
#30967=DIRECTION ( 'NONE',  ( 0.6830127018922181881, 0.6830127018922202975, -0.2588190451025214056 ) ) ;
#30968=ORIENTED_EDGE ( 'NONE', *, *, #99413, .T. ) ;
#30969=FACE_OUTER_BOUND ( 'NONE', #99228, .T. ) ;
#30970=CARTESIAN_POINT ( 'NONE',  ( -33.48921356237309510, -27.52281430457078670, 5.000000000000000000 ) ) ;
#30971=CARTESIAN_POINT ( 'NONE',  ( -36.18398860626899705, 28.73617430169812437, 5.000000000000000000 ) ) ;
#30972=DIRECTION ( 'NONE',  ( 0.6830127018922180770, -0.6830127018922204085, -0.2588190451025213501 ) ) ;
#30973=VECTOR ( 'NONE', #138881, 1000.000000000000000 ) ;
#30976=DIRECTION ( 'NONE',  ( 0.7071067811865487940, 0.7071067811865463515, -0.000000000000000000 ) ) ;
#30977=CARTESIAN_POINT ( 'NONE',  ( -9.489213562373095101, -27.52281430457062328, 5.000000000000000000 ) ) ;
#30978=ORIENTED_EDGE ( 'NONE', *, *, #29396, .T. ) ;
#30980=ORIENTED_EDGE ( 'NONE', *, *, #29487, .F. ) ;
#30982=EDGE_LOOP ( 'NONE', ( #39881, #77380, #114725 ) ) ;
#30986=ORIENTED_EDGE ( 'NONE', *, *, #97063, .F. ) ;
#30987=EDGE_LOOP ( 'NONE', ( #119462, #27613, #18962, #69536 ) ) ;
#30988=ADVANCED_FACE ( 'NONE', ( #71001 ), #59421, .F. ) ;
#30989=LINE ( 'NONE', #33153, #9471 ) ;
#30990=ADVANCED_FACE ( 'NONE', ( #138374 ), #25313, .F. ) ;
#30991=VECTOR ( 'NONE', #67750, 1000.000000000000000 ) ;
#30994=CARTESIAN_POINT ( 'NONE',  ( -32.99451991528749062, 28.92564299267960948, 4.000000000000000000 ) ) ;
#30996=CARTESIAN_POINT ( 'NONE',  ( -23.56319896779156409, -12.74070752338415069, 9.898150129686429821 ) ) ;
#30997=EDGE_CURVE ( 'NONE', #115411, #100841, #104287, .T. ) ;
#30998=FACE_OUTER_BOUND ( 'NONE', #126996, .T. ) ;
#30999=VECTOR ( 'NONE', #2004, 999.9999999999998863 ) ;
#31001=CARTESIAN_POINT ( 'NONE',  ( -14.81601139373099585, 28.73617430169776910, 5.000000000000000000 ) ) ;
#31002=ORIENTED_EDGE ( 'NONE', *, *, #93401, .T. ) ;
#31003=CARTESIAN_POINT ( 'NONE',  ( 30.51665438641024153, 22.22500000000000142, 4.500000000000000888 ) ) ;
#31004=VERTEX_POINT ( 'NONE', #103581 ) ;
#31005=EDGE_LOOP ( 'NONE', ( #38274, #105064, #132855, #73659 ) ) ;
#31008=ORIENTED_EDGE ( 'NONE', *, *, #38366, .F. ) ;
#31009=CARTESIAN_POINT ( 'NONE',  ( -33.52781275693359220, 22.22500000000000142, 4.470553524000289158 ) ) ;
#31010=CARTESIAN_POINT ( 'NONE',  ( 5.161706124526165951, -6.740707523384212863, 16.75550250614868730 ) ) ;
#31011=DIRECTION ( 'NONE',  ( -0.6830127018922181881, 0.6830127018922202975, -0.2588190451025214056 ) ) ;
#31012=ORIENTED_EDGE ( 'NONE', *, *, #7701, .F. ) ;
#31014=ORIENTED_EDGE ( 'NONE', *, *, #10048, .F. ) ;
#31015=VECTOR ( 'NONE', #86777, 1000.000000000000000 ) ;
#31016=AXIS2_PLACEMENT_3D ( 'NONE', #10348, #40859, #43011 ) ;
#31018=LINE ( 'NONE', #22232, #62375 ) ;
#31022=ORIENTED_EDGE ( 'NONE', *, *, #58409, .F. ) ;
#31023=ADVANCED_FACE ( 'NONE', ( #36221 ), #5688, .F. ) ;
#31024=EDGE_LOOP ( 'NONE', ( #51172, #9490, #4090, #24710 ) ) ;
#31025=DIRECTION ( 'NONE',  ( 1.000000000000000000, 0.000000000000000000, 0.000000000000000000 ) ) ;
#31026=DIRECTION ( 'NONE',  ( 1.000000000000000000, 0.000000000000000000, 0.000000000000000000 ) ) ;
#31027=AXIS2_PLACEMENT_3D ( 'NONE', #134416, #111949, #12609 ) ;
#31028=DIRECTION ( 'NONE',  ( -0.000000000000000000, 0.000000000000000000, 1.000000000000000000 ) ) ;
#31029=LINE ( 'NONE', #85373, #82826 ) ;
#31030=DIRECTION ( 'NONE',  ( 0.6830127018922180770, -0.6830127018922204085, -0.2588190451025213501 ) ) ;
#31033=LINE ( 'NONE', #75259, #49019 ) ;
#31035=EDGE_LOOP ( 'NONE', ( #105093, #31507, #131905, #42861 ) ) ;
#31036=LINE ( 'NONE', #9208, #46597 ) ;
#31037=CARTESIAN_POINT ( 'NONE',  ( -21.87889065874226091, 8.431076354171498366, 5.000000000000000000 ) ) ;
#31039=VECTOR ( 'NONE', #85732, 1000.000000000000000 ) ;
#31041=DIRECTION ( 'NONE',  ( 0.7071067811865487940, 0.7071067811865463515, -0.000000000000000000 ) ) ;
#31042=FACE_OUTER_BOUND ( 'NONE', #56364, .T. ) ;
#31043=ORIENTED_EDGE ( 'NONE', *, *, #138129, .T. ) ;
#31047=ORIENTED_EDGE ( 'NONE', *, *, #126142, .F. ) ;
#31048=ORIENTED_EDGE ( 'NONE', *, *, #94457, .F. ) ;
#31049=DIRECTION ( 'NONE',  ( 0.7071067811865486830, -0.7071067811865464625, -0.000000000000000000 ) ) ;
#31050=ORIENTED_EDGE ( 'NONE', *, *, #82453, .F. ) ;
#31051=VECTOR ( 'NONE', #118108, 1000.000000000000114 ) ;
#31052=EDGE_CURVE ( 'NONE', #35520, #21301, #49254, .T. ) ;
#31053=EDGE_CURVE ( 'NONE', #107783, #73971, #136222, .T. ) ;
#31058=CARTESIAN_POINT ( 'NONE',  ( 14.29289321881335795, 14.25929247661557397, 5.000000000000000000 ) ) ;
#31059=ADVANCED_FACE ( 'NONE', ( #40506 ), #19443, .F. ) ;
#31062=LINE ( 'NONE', #119446, #101724 ) ;
#31065=VECTOR ( 'NONE', #122824, 1000.000000000000000 ) ;
#31067=DIRECTION ( 'NONE',  ( -0.7071067811865486830, -0.7071067811865464625, -0.000000000000000000 ) ) ;
#31068=EDGE_LOOP ( 'NONE', ( #59240, #80088, #117285, #35405 ) ) ;
#31069=ORIENTED_EDGE ( 'NONE', *, *, #19558, .T. ) ;
#31070=ADVANCED_FACE ( 'NONE', ( #64381 ), #73141, .F. ) ;
#31071=AXIS2_PLACEMENT_3D ( 'NONE', #131892, #32586, #119544 ) ;
#31072=FACE_OUTER_BOUND ( 'NONE', #40731, .T. ) ;
#31073=VERTEX_POINT ( 'NONE', #128915 ) ;
#31074=PLANE ( 'NONE',  #136005 ) ;
#31075=AXIS2_PLACEMENT_3D ( 'NONE', #68832, #26016, #137644 ) ;
#31077=EDGE_LOOP ( 'NONE', ( #95927, #28829, #84910, #6426 ) ) ;
#31079=CARTESIAN_POINT ( 'NONE',  ( 10.49999999999993605, -20.94781430457060623, 5.000000000000000000 ) ) ;
#31080=DIRECTION ( 'NONE',  ( -0.7071067811865486830, -0.7071067811865464625, 0.000000000000000000 ) ) ;
#31081=CARTESIAN_POINT ( 'NONE',  ( 66.48921356237309510, -27.52281430457101763, 5.000000000000000000 ) ) ;
#31082=DIRECTION ( 'NONE',  ( 0.6830127018922180770, -0.6830127018922204085, -0.2588190451025213501 ) ) ;
#31084=CARTESIAN_POINT ( 'NONE',  ( 19.49999999999986855, -10.53360074219763121, 5.000000000000000000 ) ) ;
#31086=CARTESIAN_POINT ( 'NONE',  ( 0.000000000000000000, 0.000000000000000000, 5.000000000000000000 ) ) ;
#31090=ORIENTED_EDGE ( 'NONE', *, *, #72203, .T. ) ;
#31091=ORIENTED_EDGE ( 'NONE', *, *, #7019, .F. ) ;
#31092=ORIENTED_EDGE ( 'NONE', *, *, #18427, .T. ) ;
#31094=VERTEX_POINT ( 'NONE', #62254 ) ;
#31095=ADVANCED_FACE ( 'NONE', ( #84707 ), #29592, .F. ) ;
#31097=DIRECTION ( 'NONE',  ( -0.000000000000000000, 0.3543493200069153248, 0.9351131265310292928 ) ) ;
#31098=VERTEX_POINT ( 'NONE', #119444 ) ;
#31099=LINE ( 'NONE', #121640, #16652 ) ;
#31100=DIRECTION ( 'NONE',  ( 0.3543493200069162685, -0.000000000000000000, -0.9351131265310288487 ) ) ;
#31101=VECTOR ( 'NONE', #21855, 999.9999999999998863 ) ;
#31102=EDGE_CURVE ( 'NONE', #46563, #114228, #65121, .T. ) ;
#31104=ORIENTED_EDGE ( 'NONE', *, *, #135501, .F. ) ;
#31105=EDGE_CURVE ( 'NONE', #105446, #54652, #74560, .T. ) ;
#31106=CARTESIAN_POINT ( 'NONE',  ( 48.18398860626899705, 28.73617430169820608, 5.000000000000000000 ) ) ;
#31109=CARTESIAN_POINT ( 'NONE',  ( -45.48921356237309510, -27.52281430457087197, 5.000000000000000000 ) ) ;
#31110=EDGE_CURVE ( 'NONE', #47599, #45624, #131068, .T. ) ;
#31113=ORIENTED_EDGE ( 'NONE', *, *, #35551, .T. ) ;
#31114=DIRECTION ( 'NONE',  ( 1.000000000000000000, 0.000000000000000000, 0.000000000000000000 ) ) ;
#31115=LINE ( 'NONE', #8574, #68688 ) ;
#31117=VECTOR ( 'NONE', #66118, 1000.000000000000000 ) ;
#31118=CARTESIAN_POINT ( 'NONE',  ( -8.510786437626906675, -27.52281430457049183, 5.000000000000000000 ) ) ;
#31119=DIRECTION ( 'NONE',  ( -0.6830127018922181881, 0.6830127018922202975, -0.2588190451025214056 ) ) ;
#31121=AXIS2_PLACEMENT_3D ( 'NONE', #111445, #143362, #20141 ) ;
#31122=VERTEX_POINT ( 'NONE', #41929 ) ;
#31123=( BOUNDED_CURVE ( )  B_SPLINE_CURVE ( 3, ( #105872, #126234, #95001, #82050 ),
 .UNSPECIFIED., .F., .T. ) 
 B_SPLINE_CURVE_WITH_KNOTS ( ( 4, 4 ),
 ( 5.920967161967926273, 7.341195215986587641 ),
 .UNSPECIFIED. ) 
 CURVE ( )  GEOMETRIC_REPRESENTATION_ITEM ( )  RATIONAL_B_SPLINE_CURVE ( ( 1.000000000000000000, 0.8388583629366720418, 0.8388583629366720418, 1.000000000000000000 ) ) 
 REPRESENTATION_ITEM ( '' )  );
#31124=ORIENTED_EDGE ( 'NONE', *, *, #116696, .F. ) ;
#31126=DIRECTION ( 'NONE',  ( 0.6830127018922181881, 0.6830127018922202975, -0.2588190451025214056 ) ) ;
#31127=ORIENTED_EDGE ( 'NONE', *, *, #35558, .T. ) ;
#31128=ORIENTED_EDGE ( 'NONE', *, *, #118076, .F. ) ;
#31129=ADVANCED_FACE ( 'NONE', ( #31757 ), #96961, .F. ) ;
#31131=DIRECTION ( 'NONE',  ( -0.7071067811865487940, 0.7071067811865463515, 0.000000000000000000 ) ) ;
#31132=ORIENTED_EDGE ( 'NONE', *, *, #100401, .T. ) ;
#31133=AXIS2_PLACEMENT_3D ( 'NONE', #121570, #45488, #89665 ) ;
#31136=VECTOR ( 'NONE', #18205, 1000.000000000000000 ) ;
#31137=DIRECTION ( 'NONE',  ( -0.7071067811865487940, 0.7071067811865463515, 0.000000000000000000 ) ) ;
#31138=CARTESIAN_POINT ( 'NONE',  ( -34.92500000000001137, 8.816654386410331057, 4.500000000000000888 ) ) ;
#31139=DIRECTION ( 'NONE',  ( -0.7071067811865487940, 0.7071067811865463515, 0.000000000000000000 ) ) ;
#31143=ORIENTED_EDGE ( 'NONE', *, *, #38419, .F. ) ;
#31145=LINE ( 'NONE', #75359, #96689 ) ;
#31148=VERTEX_POINT ( 'NONE', #109308 ) ;
#31149=DIRECTION ( 'NONE',  ( -0.000000000000000000, 0.3543493200069153248, 0.9351131265310292928 ) ) ;
#31150=EDGE_LOOP ( 'NONE', ( #104924, #54101, #43377, #134158 ) ) ;
#31151=ORIENTED_EDGE ( 'NONE', *, *, #19232, .F. ) ;
#31154=VECTOR ( 'NONE', #27371, 1000.000000000000227 ) ;
#31156=FACE_OUTER_BOUND ( 'NONE', #60647, .T. ) ;
#31158=CARTESIAN_POINT ( 'NONE',  ( 6.792893218813416567, -14.24070752338413826, 5.000000000000000000 ) ) ;
#31159=DIRECTION ( 'NONE',  ( -0.000000000000000000, 0.000000000000000000, 1.000000000000000000 ) ) ;
#31160=LINE ( 'NONE', #75369, #11401 ) ;
#31161=CARTESIAN_POINT ( 'NONE',  ( -22.17183060077631396, 12.75929247661558996, 4.000000000000000000 ) ) ;
#31162=DIRECTION ( 'NONE',  ( -0.000000000000000000, 0.000000000000000000, 1.000000000000000000 ) ) ;
#31163=PLANE ( 'NONE',  #110600 ) ;
#31164=LINE ( 'NONE', #141325, #58500 ) ;
#31165=DIRECTION ( 'NONE',  ( 0.6830127018922180770, -0.6830127018922204085, -0.2588190451025213501 ) ) ;
#31166=LINE ( 'NONE', #31864, #99177 ) ;
#31167=LINE ( 'NONE', #30441, #12346 ) ;
#31168=ORIENTED_EDGE ( 'NONE', *, *, #65388, .T. ) ;
#31169=VERTEX_POINT ( 'NONE', #120145 ) ;
#31171=ORIENTED_EDGE ( 'NONE', *, *, #59376, .F. ) ;
#31172=PLANE ( 'NONE',  #132903 ) ;
#31173=VERTEX_POINT ( 'NONE', #86139 ) ;
#31174=ORIENTED_EDGE ( 'NONE', *, *, #126256, .T. ) ;
#31175=CARTESIAN_POINT ( 'NONE',  ( 21.18398860626899349, 28.73617430169802134, 5.000000000000000000 ) ) ;
#31176=DIRECTION ( 'NONE',  ( -1.000000000000000000, 0.000000000000000000, -0.000000000000000000 ) ) ;
#31177=DIRECTION ( 'NONE',  ( 0.7071067811865486830, -0.7071067811865464625, -0.000000000000000000 ) ) ;
#31178=ORIENTED_EDGE ( 'NONE', *, *, #23028, .F. ) ;
#31179=CARTESIAN_POINT ( 'NONE',  ( 11.99999999999991651, -12.41253812416062985, 4.000000000000000000 ) ) ;
#31180=ORIENTED_EDGE ( 'NONE', *, *, #40698, .T. ) ;
#31181=DIRECTION ( 'NONE',  ( 0.7071067811865487940, 0.7071067811865463515, -0.000000000000000000 ) ) ;
#31182=DIRECTION ( 'NONE',  ( 0.7071067811865487940, -0.7071067811865463515, 0.000000000000000000 ) ) ;
#31184=ORIENTED_EDGE ( 'NONE', *, *, #71887, .F. ) ;
#31187=DIRECTION ( 'NONE',  ( -0.7071067811865486830, 0.7071067811865464625, 0.000000000000000000 ) ) ;
#31188=LINE ( 'NONE', #75405, #79042 ) ;
#31189=ORIENTED_EDGE ( 'NONE', *, *, #68640, .F. ) ;
#31190=ORIENTED_EDGE ( 'NONE', *, *, #30250, .T. ) ;
#31192=ORIENTED_EDGE ( 'NONE', *, *, #119877, .T. ) ;
#31193=LINE ( 'NONE', #62401, #25500 ) ;
#31194=DIRECTION ( 'NONE',  ( 0.000000000000000000, 0.3543493200069153248, 0.9351131265310291818 ) ) ;
#31195=FACE_OUTER_BOUND ( 'NONE', #25236, .T. ) ;
#31196=CARTESIAN_POINT ( 'NONE',  ( 20.99451991528748707, 28.92564299267952777, 4.000000000000000000 ) ) ;
#31197=AXIS2_PLACEMENT_3D ( 'NONE', #99969, #55767, #108656 ) ;
#31198=ORIENTED_EDGE ( 'NONE', *, *, #142652, .F. ) ;
#31200=DIRECTION ( 'NONE',  ( -0.3543493200069162685, -0.000000000000000000, -0.9351131265310288487 ) ) ;
#31202=ADVANCED_FACE ( 'NONE', ( #63693 ), #84029, .F. ) ;
#31203=VERTEX_POINT ( 'NONE', #108552 ) ;
#31204=LINE ( 'NONE', #139267, #79117 ) ;
#31205=DIRECTION ( 'NONE',  ( 0.7071067811865487940, 0.7071067811865463515, 0.000000000000000000 ) ) ;
#31206=EDGE_LOOP ( 'NONE', ( #39720, #60784, #101843, #7307 ) ) ;
#31207=CARTESIAN_POINT ( 'NONE',  ( -12.69326993309591245, -3.740707523384244837, 12.88036043432870592 ) ) ;
#31208=ORIENTED_EDGE ( 'NONE', *, *, #35306, .F. ) ;
#31209=VERTEX_POINT ( 'NONE', #95572 ) ;
#31210=EDGE_CURVE ( 'NONE', #86264, #53831, #9993, .T. ) ;
#31211=EDGE_CURVE ( 'NONE', #141704, #67140, #117306, .T. ) ;
#31212=LINE ( 'NONE', #40659, #28470 ) ;
#31213=LINE ( 'NONE', #75429, #22912 ) ;
#31214=ORIENTED_EDGE ( 'NONE', *, *, #56724, .T. ) ;
#31215=DIRECTION ( 'NONE',  ( -0.000000000000000000, 0.3543493200069153248, 0.9351131265310292928 ) ) ;
#31216=EDGE_CURVE ( 'NONE', #21579, #15722, #46232, .T. ) ;
#31217=EDGE_CURVE ( 'NONE', #38500, #44746, #132535, .T. ) ;
#31218=DIRECTION ( 'NONE',  ( 0.7071067811865487940, 0.7071067811865463515, 0.000000000000000000 ) ) ;
#31219=VECTOR ( 'NONE', #102400, 999.9999999999998863 ) ;
#31220=CARTESIAN_POINT ( 'NONE',  ( -16.17183060077635659, -11.24070752338416135, 4.000000000000000000 ) ) ;
#31221=PLANE ( 'NONE',  #13731 ) ;
#31222=AXIS2_PLACEMENT_3D ( 'NONE', #34269, #77780, #122687 ) ;
#31225=CARTESIAN_POINT ( 'NONE',  ( 78.18398860626899705, 28.73617430169841924, 5.000000000000000000 ) ) ;
#31226=CARTESIAN_POINT ( 'NONE',  ( -31.17183060077625356, -20.24070752338407075, 4.000000000000000000 ) ) ;
#31227=CARTESIAN_POINT ( 'NONE',  ( -6.489213562373093325, -27.52281430457059841, 5.000000000000000000 ) ) ;
#31228=CARTESIAN_POINT ( 'NONE',  ( 22.17183060077631040, -14.24070752338414358, 4.000000000000000000 ) ) ;
#31229=CARTESIAN_POINT ( 'NONE',  ( 32.99999999999977263, -21.03360074219752107, 5.000000000000000000 ) ) ;
#31230=CARTESIAN_POINT ( 'NONE',  ( -24.29974487139158867, -27.71228299555223273, 4.000000000000000000 ) ) ;
#31231=ADVANCED_FACE ( 'NONE', ( #56411 ), #45520, .F. ) ;
#31232=DIRECTION ( 'NONE',  ( 1.000000000000000000, 0.000000000000000000, 0.000000000000000000 ) ) ;
#31233=DIRECTION ( 'NONE',  ( 0.7071067811865487940, -0.7071067811865463515, 0.000000000000000000 ) ) ;
#31235=ORIENTED_EDGE ( 'NONE', *, *, #12518, .T. ) ;
#31236=VERTEX_POINT ( 'NONE', #23731 ) ;
#31238=EDGE_CURVE ( 'NONE', #35758, #98113, #68003, .T. ) ;
#31240=VECTOR ( 'NONE', #30114, 1000.000000000000000 ) ;
#31242=VERTEX_POINT ( 'NONE', #100594 ) ;
#31243=CARTESIAN_POINT ( 'NONE',  ( 20.51078643762690490, -27.52281430457041012, 5.000000000000000000 ) ) ;
#31244=CARTESIAN_POINT ( 'NONE',  ( -21.18398860626899349, 28.73617430169802134, 5.000000000000000000 ) ) ;
#31245=ORIENTED_EDGE ( 'NONE', *, *, #24979, .F. ) ;
#31246=DIRECTION ( 'NONE',  ( -0.7071067811865486830, -0.7071067811865464625, -0.000000000000000000 ) ) ;
#31248=CARTESIAN_POINT ( 'NONE',  ( 34.92499999999998295, -21.72500000000000142, 5.000000000000000000 ) ) ;
#31249=CARTESIAN_POINT ( 'NONE',  ( 2.999999999999985345, -0.8619312979531966734, -5.102805207349819128 ) ) ;
#31251=VERTEX_POINT ( 'NONE', #11380 ) ;
#31252=DIRECTION ( 'NONE',  ( -0.7071067811865486830, -0.7071067811865464625, -0.000000000000000000 ) ) ;
#31253=DIRECTION ( 'NONE',  ( 0.6830127018922181881, 0.6830127018922202975, -0.2588190451025214056 ) ) ;
#31255=EDGE_CURVE ( 'NONE', #141655, #93537, #44067, .T. ) ;
#31256=CARTESIAN_POINT ( 'NONE',  ( -32.99999999999977263, -13.06887692260767686, 4.000000000000000000 ) ) ;
#31257=DIRECTION ( 'NONE',  ( -0.000000000000000000, -0.3543493200069152693, 0.9351131265310292928 ) ) ;
#31260=VECTOR ( 'NONE', #92367, 1000.000000000000000 ) ;
#31261=VECTOR ( 'NONE', #64875, 1000.000000000000000 ) ;
#31266=ORIENTED_EDGE ( 'NONE', *, *, #2129, .T. ) ;
#31268=ADVANCED_FACE ( 'NONE', ( #76717 ), #134661, .F. ) ;
#31271=DIRECTION ( 'NONE',  ( 0.7071067811865487940, 0.7071067811865463515, -0.000000000000000000 ) ) ;
#31272=CARTESIAN_POINT ( 'NONE',  ( -0.4892135623730947680, -27.52281430457055578, 5.000000000000000000 ) ) ;
#31276=EDGE_CURVE ( 'NONE', #24394, #135463, #123055, .T. ) ;
#31277=CARTESIAN_POINT ( 'NONE',  ( 69.18398860626899705, 28.73617430169835529, 5.000000000000000000 ) ) ;
#31278=ORIENTED_EDGE ( 'NONE', *, *, #50510, .F. ) ;
#31279=DIRECTION ( 'NONE',  ( -0.7071067811865486830, -0.7071067811865464625, 0.000000000000000000 ) ) ;
#31280=DIRECTION ( 'NONE',  ( -0.000000000000000000, -0.3543493200069152693, 0.9351131265310292928 ) ) ;
#31282=ADVANCED_FACE ( 'NONE', ( #43351 ), #87563, .F. ) ;
#31283=EDGE_CURVE ( 'NONE', #56496, #39354, #143361, .T. ) ;
#31284=LINE ( 'NONE', #74807, #95069 ) ;
#31285=ORIENTED_EDGE ( 'NONE', *, *, #103521, .T. ) ;
#31287=ORIENTED_EDGE ( 'NONE', *, *, #63632, .T. ) ;
#31288=LINE ( 'NONE', #129872, #19296 ) ;
#31289=CARTESIAN_POINT ( 'NONE',  ( -34.92500000000001137, -22.22500000000000142, 4.000000000000000000 ) ) ;
#31290=DIRECTION ( 'NONE',  ( -0.7071067811865486830, -0.7071067811865464625, -0.000000000000000000 ) ) ;
#31293=ORIENTED_EDGE ( 'NONE', *, *, #80129, .T. ) ;
#31297=ORIENTED_EDGE ( 'NONE', *, *, #53998, .T. ) ;
#31298=ORIENTED_EDGE ( 'NONE', *, *, #35385, .T. ) ;
#31299=DIRECTION ( 'NONE',  ( -0.6830127018922180770, -0.6830127018922204085, -0.2588190451025213501 ) ) ;
#31300=ORIENTED_EDGE ( 'NONE', *, *, #17370, .F. ) ;
#31301=LINE ( 'NONE', #100122, #55341 ) ;
#31302=LINE ( 'NONE', #47224, #128863 ) ;
#31303=DIRECTION ( 'NONE',  ( -1.000000000000000000, 0.000000000000000000, 0.000000000000000000 ) ) ;
#31304=DIRECTION ( 'NONE',  ( -0.7071067811865486830, 0.7071067811865464625, 0.000000000000000000 ) ) ;
#31305=FACE_BOUND ( 'NONE', #15595, .T. ) ;
#31306=ORIENTED_EDGE ( 'NONE', *, *, #44972, .F. ) ;
#31308=CARTESIAN_POINT ( 'NONE',  ( -23.70025512860841133, -27.71228299555189523, 4.000000000000000000 ) ) ;
#31309=CARTESIAN_POINT ( 'NONE',  ( -34.42500000000001137, -21.72500000000000142, 0.4999999999999995559 ) ) ;
#31310=VERTEX_POINT ( 'NONE', #14982 ) ;
#31311=DIRECTION ( 'NONE',  ( 0.6830127018922181881, 0.6830127018922202975, -0.2588190451025214056 ) ) ;
#31312=ORIENTED_EDGE ( 'NONE', *, *, #81716, .T. ) ;
#31313=ORIENTED_EDGE ( 'NONE', *, *, #45875, .F. ) ;
#31314=DIRECTION ( 'NONE',  ( -1.000000000000000000, 0.000000000000000000, 0.000000000000000000 ) ) ;
#31315=ORIENTED_EDGE ( 'NONE', *, *, #128570, .T. ) ;
#31316=AXIS2_PLACEMENT_3D ( 'NONE', #73858, #130392, #96279 ) ;
#31318=ORIENTED_EDGE ( 'NONE', *, *, #84969, .T. ) ;
#31319=DIRECTION ( 'NONE',  ( 0.7071067811865486830, -0.7071067811865464625, -0.000000000000000000 ) ) ;
#31320=ORIENTED_EDGE ( 'NONE', *, *, #30960, .T. ) ;
#31321=VECTOR ( 'NONE', #34633, 1000.000000000000000 ) ;
#31322=DIRECTION ( 'NONE',  ( -0.000000000000000000, 0.000000000000000000, 1.000000000000000000 ) ) ;
#31323=ORIENTED_EDGE ( 'NONE', *, *, #42, .T. ) ;
#31325=DIRECTION ( 'NONE',  ( -0.6830127018922181881, 0.6830127018922202975, -0.2588190451025214056 ) ) ;
#31326=ADVANCED_FACE ( 'NONE', ( #91158 ), #25143, .F. ) ;
#31327=EDGE_CURVE ( 'NONE', #6816, #100625, #36741, .T. ) ;
#31328=FACE_OUTER_BOUND ( 'NONE', #142482, .T. ) ;
#31329=VECTOR ( 'NONE', #42106, 1000.000000000000000 ) ;
#31330=CARTESIAN_POINT ( 'NONE',  ( 24.29974487139158867, -27.71228299555223273, 4.000000000000000000 ) ) ;
#31331=CARTESIAN_POINT ( 'NONE',  ( -3.489213562373097322, -27.52281430457057709, 5.000000000000000000 ) ) ;
#31332=FACE_OUTER_BOUND ( 'NONE', #117730, .T. ) ;
#31333=ORIENTED_EDGE ( 'NONE', *, *, #131492, .F. ) ;
#31337=PLANE ( 'NONE',  #99909 ) ;
#31338=ORIENTED_EDGE ( 'NONE', *, *, #17825, .F. ) ;
#31339=ORIENTED_EDGE ( 'NONE', *, *, #80533, .T. ) ;
#31340=VERTEX_POINT ( 'NONE', #138211 ) ;
#31341=CARTESIAN_POINT ( 'NONE',  ( -26.67183060077628198, -21.74070752338406010, 4.000000000000000000 ) ) ;
#31342=CARTESIAN_POINT ( 'NONE',  ( -3.328169399223505742, 11.25929247661559707, 4.000000000000000000 ) ) ;
#31343=EDGE_CURVE ( 'NONE', #84739, #66605, #4057, .T. ) ;
#31344=LINE ( 'NONE', #8805, #90183 ) ;
#31345=EDGE_LOOP ( 'NONE', ( #90755, #38748, #129004, #89095 ) ) ;
#31346=CARTESIAN_POINT ( 'NONE',  ( 14.81601139373099585, 28.73617430169776910, 5.000000000000000000 ) ) ;
#31347=VECTOR ( 'NONE', #67472, 1000.000000000000000 ) ;
#31348=CARTESIAN_POINT ( 'NONE',  ( -15.79076468313838433, 8.175634574663693144, 5.000000000000000000 ) ) ;
#31349=VECTOR ( 'NONE', #111948, 1000.000000000000227 ) ;
#31352=AXIS2_PLACEMENT_3D ( 'NONE', #123976, #45024, #88499 ) ;
#31354=ORIENTED_EDGE ( 'NONE', *, *, #46441, .T. ) ;
#31356=DIRECTION ( 'NONE',  ( 0.6830127018922180770, -0.6830127018922204085, -0.2588190451025213501 ) ) ;
#31357=DIRECTION ( 'NONE',  ( -0.000000000000000000, -0.3543493200069153248, -0.9351131265310291818 ) ) ;
#31358=CARTESIAN_POINT ( 'NONE',  ( 28.49999999999980460, 13.08746187583912146, 4.000000000000000000 ) ) ;
#31361=EDGE_LOOP ( 'NONE', ( #86868, #49523, #41157, #11995 ) ) ;
#31362=CARTESIAN_POINT ( 'NONE',  ( 0.4892135623730947680, -27.52281430457055578, 5.000000000000000000 ) ) ;
#31364=DIRECTION ( 'NONE',  ( 0.6830127018922181881, 0.6830127018922202975, -0.2588190451025214056 ) ) ;
#31367=DIRECTION ( 'NONE',  ( 0.7071067811865486830, -0.7071067811865464625, -0.000000000000000000 ) ) ;
#31368=EDGE_LOOP ( 'NONE', ( #114126, #134418, #69377, #7732 ) ) ;
#31370=DIRECTION ( 'NONE',  ( -0.000000000000000000, 0.3543493200069153248, 0.9351131265310292928 ) ) ;
#31371=VERTEX_POINT ( 'NONE', #83118 ) ;
#31372=LINE ( 'NONE', #75597, #123579 ) ;
#31373=DIRECTION ( 'NONE',  ( -1.000000000000000000, 0.000000000000000000, -0.000000000000000000 ) ) ;
#31374=ORIENTED_EDGE ( 'NONE', *, *, #143083, .T. ) ;
#31375=EDGE_CURVE ( 'NONE', #126278, #137809, #48342, .T. ) ;
#31376=ORIENTED_EDGE ( 'NONE', *, *, #111669, .F. ) ;
#31377=FACE_OUTER_BOUND ( 'NONE', #105668, .T. ) ;
#31380=EDGE_CURVE ( 'NONE', #50767, #126713, #70143, .T. ) ;
#31381=CARTESIAN_POINT ( 'NONE',  ( 39.48921356237310221, -27.52281430457082934, 5.000000000000000000 ) ) ;
#31383=EDGE_CURVE ( 'NONE', #36965, #68527, #127319, .T. ) ;
#31384=VERTEX_POINT ( 'NONE', #16393 ) ;
#31386=ADVANCED_FACE ( 'NONE', ( #38897 ), #38199, .F. ) ;
#31387=DIRECTION ( 'NONE',  ( -0.6830127018922180770, -0.6830127018922202975, -0.2588190451025213501 ) ) ;
#31390=ADVANCED_FACE ( 'NONE', ( #36059 ), #80981, .F. ) ;
#31392=LINE ( 'NONE', #106786, #78871 ) ;
#31393=ORIENTED_EDGE ( 'NONE', *, *, #23006, .F. ) ;
#31394=ORIENTED_EDGE ( 'NONE', *, *, #140645, .F. ) ;
#31396=EDGE_CURVE ( 'NONE', #89130, #35044, #16680, .T. ) ;
#31399=ORIENTED_EDGE ( 'NONE', *, *, #136704, .F. ) ;
#31400=PLANE ( 'NONE',  #117355 ) ;
#31401=DIRECTION ( 'NONE',  ( -0.3543493200069162685, -0.000000000000000000, -0.9351131265310288487 ) ) ;
#31402=ORIENTED_EDGE ( 'NONE', *, *, #80290, .T. ) ;
#31404=DIRECTION ( 'NONE',  ( -0.7071067811865486830, -0.7071067811865464625, -0.000000000000000000 ) ) ;
#31405=LINE ( 'NONE', #9616, #141519 ) ;
#31406=EDGE_CURVE ( 'NONE', #90585, #87703, #5523, .T. ) ;
#31407=DIRECTION ( 'NONE',  ( -0.3543493200069162685, -0.000000000000000000, -0.9351131265310288487 ) ) ;
#31408=ADVANCED_FACE ( 'NONE', ( #136058 ), #28022, .F. ) ;
#31409=DIRECTION ( 'NONE',  ( 1.000000000000000000, 0.000000000000000000, 0.000000000000000000 ) ) ;
#31411=ORIENTED_EDGE ( 'NONE', *, *, #98008, .T. ) ;
#31412=LINE ( 'NONE', #98780, #125204 ) ;
#31413=DIRECTION ( 'NONE',  ( -0.6830127018922180770, -0.6830127018922204085, -0.2588190451025213501 ) ) ;
#31415=PLANE ( 'NONE',  #71071 ) ;
#31416=CARTESIAN_POINT ( 'NONE',  ( 20.20710678118640402, -17.24070752338410628, 5.000000000000000000 ) ) ;
#31417=ADVANCED_FACE ( 'NONE', ( #13539 ), #2671, .F. ) ;
#31419=LINE ( 'NONE', #43014, #13382 ) ;
#31421=AXIS2_PLACEMENT_3D ( 'NONE', #123994, #70363, #47884 ) ;
#31423=ORIENTED_EDGE ( 'NONE', *, *, #56638, .T. ) ;
#31424=ORIENTED_EDGE ( 'NONE', *, *, #104853, .F. ) ;
#31427=VECTOR ( 'NONE', #141829, 1000.000000000000000 ) ;
#31428=CARTESIAN_POINT ( 'NONE',  ( -0.4892135623730947680, -27.52281430457055578, 5.000000000000000000 ) ) ;
#31429=FACE_OUTER_BOUND ( 'NONE', #82038, .T. ) ;
#31430=ORIENTED_EDGE ( 'NONE', *, *, #67597, .T. ) ;
#31431=CARTESIAN_POINT ( 'NONE',  ( 0.4892135623730947680, -27.52281430457055578, 5.000000000000000000 ) ) ;
#31432=CARTESIAN_POINT ( 'NONE',  ( 13.22578070446010301, 4.485909045323550615, 4.327832195654622183 ) ) ;
#31434=ORIENTED_EDGE ( 'NONE', *, *, #1438, .T. ) ;
#31436=CARTESIAN_POINT ( 'NONE',  ( -69.18398860626899705, 28.73617430169835529, 5.000000000000000000 ) ) ;
#31437=ORIENTED_EDGE ( 'NONE', *, *, #91541, .T. ) ;
#31438=ORIENTED_EDGE ( 'NONE', *, *, #61794, .T. ) ;
#31439=DIRECTION ( 'NONE',  ( -0.7071067811865486830, -0.7071067811865464625, -0.000000000000000000 ) ) ;
#31440=DIRECTION ( 'NONE',  ( 0.7071067811865486830, -0.7071067811865464625, -0.000000000000000000 ) ) ;
#31441=CARTESIAN_POINT ( 'NONE',  ( -34.92500000000001137, 11.07784511950552897, 0.7759263132492092430 ) ) ;
#31442=DIRECTION ( 'NONE',  ( -0.7071067811865486830, -0.7071067811865464625, 0.000000000000000000 ) ) ;
#31443=ORIENTED_EDGE ( 'NONE', *, *, #27144, .F. ) ;
#31444=CARTESIAN_POINT ( 'NONE',  ( 18.98155265364318822, 18.75929247661551713, 20.33588619593438551 ) ) ;
#31448=DIRECTION ( 'NONE',  ( -0.3543493200069162685, -0.000000000000000000, -0.9351131265310288487 ) ) ;
#31449=DIRECTION ( 'NONE',  ( 0.7071067811865486830, -0.7071067811865464625, -0.000000000000000000 ) ) ;
#31450=LINE ( 'NONE', #64797, #74874 ) ;
#31451=CARTESIAN_POINT ( 'NONE',  ( 30.32816939922332011, 8.259292476615630818, 4.000000000000000000 ) ) ;
#31453=EDGE_CURVE ( 'NONE', #117034, #3157, #19284, .T. ) ;
#31455=VECTOR ( 'NONE', #86544, 1000.000000000000000 ) ;
#31456=ORIENTED_EDGE ( 'NONE', *, *, #49280, .T. ) ;
#31457=DIRECTION ( 'NONE',  ( -0.000000000000000000, 0.000000000000000000, 1.000000000000000000 ) ) ;
#31459=CARTESIAN_POINT ( 'NONE',  ( 0.000000000000000000, 0.000000000000000000, 5.000000000000000000 ) ) ;
#31460=EDGE_CURVE ( 'NONE', #53079, #119580, #83863, .T. ) ;
#31462=CARTESIAN_POINT ( 'NONE',  ( -18.48921356237309510, -27.52281430457068367, 5.000000000000000000 ) ) ;
#31463=EDGE_LOOP ( 'NONE', ( #21275, #26737, #73452, #129064 ) ) ;
#31464=VERTEX_POINT ( 'NONE', #108386 ) ;
#31466=DIRECTION ( 'NONE',  ( -0.7071067811865487940, 0.7071067811865463515, -0.000000000000000000 ) ) ;
#31467=CARTESIAN_POINT ( 'NONE',  ( -6.812461875839420422, -22.22500000000000142, 4.000000000000000000 ) ) ;
#31469=VERTEX_POINT ( 'NONE', #42496 ) ;
#31470=EDGE_CURVE ( 'NONE', #91708, #75295, #119295, .T. ) ;
#31473=DIRECTION ( 'NONE',  ( 0.3543493200069163240, 0.000000000000000000, 0.9351131265310288487 ) ) ;
#31475=PLANE ( 'NONE',  #48945 ) ;
#31476=EDGE_CURVE ( 'NONE', #105871, #24821, #128068, .T. ) ;
#31477=FACE_BOUND ( 'NONE', #137789, .T. ) ;
#31478=LINE ( 'NONE', #109006, #138210 ) ;
#31480=LINE ( 'NONE', #107594, #36414 ) ;
#31482=ORIENTED_EDGE ( 'NONE', *, *, #77391, .T. ) ;
#31483=DIRECTION ( 'NONE',  ( -0.000000000000000000, -0.3543493200069152693, 0.9351131265310292928 ) ) ;
#31485=ORIENTED_EDGE ( 'NONE', *, *, #124808, .F. ) ;
#31486=EDGE_LOOP ( 'NONE', ( #6829, #73942, #82691, #12660 ) ) ;
#31488=VERTEX_POINT ( 'NONE', #53327 ) ;
#31489=CARTESIAN_POINT ( 'NONE',  ( -14.99999999999989875, -4.447814304570775867, 5.000000000000000000 ) ) ;
#31490=DIRECTION ( 'NONE',  ( -0.7071067811865486830, -0.7071067811865464625, 0.000000000000000000 ) ) ;
#31491=ORIENTED_EDGE ( 'NONE', *, *, #89506, .T. ) ;
#31492=DIRECTION ( 'NONE',  ( 0.7071067811865487940, 0.7071067811865463515, -0.000000000000000000 ) ) ;
#31493=DIRECTION ( 'NONE',  ( -1.000000000000000000, 0.000000000000000000, 0.000000000000000000 ) ) ;
#31495=EDGE_CURVE ( 'NONE', #14271, #107195, #107707, .T. ) ;
#31496=CARTESIAN_POINT ( 'NONE',  ( -27.79289321881325492, 18.75929247661552068, 5.000000000000000000 ) ) ;
#31497=LINE ( 'NONE', #120612, #6407 ) ;
#31498=DIRECTION ( 'NONE',  ( 0.3543493200069162685, -0.000000000000000000, -0.9351131265310288487 ) ) ;
#31499=CARTESIAN_POINT ( 'NONE',  ( 24.48921356237309510, -27.52281430457072631, 5.000000000000000000 ) ) ;
#31500=CARTESIAN_POINT ( 'NONE',  ( 12.18398860626900060, 28.73617430169795739, 5.000000000000000000 ) ) ;
#31501=ORIENTED_EDGE ( 'NONE', *, *, #138147, .T. ) ;
#31502=CARTESIAN_POINT ( 'NONE',  ( 34.49999999999976552, -10.91253812416064584, 4.000000000000000000 ) ) ;
#31503=ORIENTED_EDGE ( 'NONE', *, *, #88518, .F. ) ;
#31505=FACE_OUTER_BOUND ( 'NONE', #19792, .T. ) ;
#31506=ORIENTED_EDGE ( 'NONE', *, *, #19855, .T. ) ;
#31507=ORIENTED_EDGE ( 'NONE', *, *, #112468, .F. ) ;
#31508=ADVANCED_FACE ( 'NONE', ( #9069 ), #30895, .F. ) ;
#31509=ORIENTED_EDGE ( 'NONE', *, *, #31476, .F. ) ;
#31511=ORIENTED_EDGE ( 'NONE', *, *, #112131, .F. ) ;
#31512=DIRECTION ( 'NONE',  ( 0.7071067811865487940, 0.7071067811865463515, -0.000000000000000000 ) ) ;
#31514=DIRECTION ( 'NONE',  ( -0.7071067811865486830, -0.7071067811865464625, 0.000000000000000000 ) ) ;
#31516=( BOUNDED_CURVE ( )  B_SPLINE_CURVE ( 3, ( #36761, #125937, #104135, #92555 ),
 .UNSPECIFIED., .F., .T. ) 
 B_SPLINE_CURVE_WITH_KNOTS ( ( 4, 4 ),
 ( 5.143245962375977420, 6.645403452391244414 ),
 .UNSPECIFIED. ) 
 CURVE ( )  GEOMETRIC_REPRESENTATION_ITEM ( )  RATIONAL_B_SPLINE_CURVE ( ( 1.000000000000000000, 0.8206354192515272761, 0.8206354192515272761, 1.000000000000000000 ) ) 
 REPRESENTATION_ITEM ( '' )  );
#31518=ORIENTED_EDGE ( 'NONE', *, *, #109343, .T. ) ;
#31519=AXIS2_PLACEMENT_3D ( 'NONE', #18393, #76397, #29297 ) ;
#31521=EDGE_LOOP ( 'NONE', ( #89807, #86270, #71657, #128982 ) ) ;
#31523=LINE ( 'NONE', #20621, #31261 ) ;
#31524=CARTESIAN_POINT ( 'NONE',  ( 54.48921356237310221, -27.52281430457093236, 5.000000000000000000 ) ) ;
#31525=VERTEX_POINT ( 'NONE', #72996 ) ;
#31526=VERTEX_POINT ( 'NONE', #40351 ) ;
#31527=CARTESIAN_POINT ( 'NONE',  ( 2.700255128608413990, -27.71228299555204089, 4.000000000000000000 ) ) ;
#31528=EDGE_CURVE ( 'NONE', #85826, #98772, #50491, .T. ) ;
#31529=LINE ( 'NONE', #62033, #70043 ) ;
#31530=DIRECTION ( 'NONE',  ( 0.7071067811865486830, -0.7071067811865464625, -0.000000000000000000 ) ) ;
#31533=ORIENTED_EDGE ( 'NONE', *, *, #79005, .F. ) ;
#31534=ORIENTED_EDGE ( 'NONE', *, *, #99759, .F. ) ;
#31535=ORIENTED_EDGE ( 'NONE', *, *, #2100, .T. ) ;
#31537=CARTESIAN_POINT ( 'NONE',  ( -34.92500000000001137, -20.24070752338407786, 4.255531930566252896 ) ) ;
#31538=CARTESIAN_POINT ( 'NONE',  ( 34.92499999999998295, 11.71849043720414052, 4.759050581649325373 ) ) ;
#31540=LINE ( 'NONE', #98911, #116397 ) ;
#31541=CARTESIAN_POINT ( 'NONE',  ( 45.48921356237309510, -27.52281430457087197, 5.000000000000000000 ) ) ;
#31542=LINE ( 'NONE', #85911, #104910 ) ;
#31543=VECTOR ( 'NONE', #18570, 999.9999999999998863 ) ;
#31545=VERTEX_POINT ( 'NONE', #41037 ) ;
#31547=VERTEX_POINT ( 'NONE', #51211 ) ;
#31550=VECTOR ( 'NONE', #101697, 1000.000000000000114 ) ;
#31551=LINE ( 'NONE', #10484, #127175 ) ;
#31552=VECTOR ( 'NONE', #101470, 1000.000000000000000 ) ;
#31553=EDGE_CURVE ( 'NONE', #69963, #98666, #105553, .T. ) ;
#31554=ORIENTED_EDGE ( 'NONE', *, *, #120691, .T. ) ;
#31555=LINE ( 'NONE', #88076, #59997 ) ;
#31557=ORIENTED_EDGE ( 'NONE', *, *, #86218, .T. ) ;
#31559=ORIENTED_EDGE ( 'NONE', *, *, #59723, .T. ) ;
#31560=FACE_OUTER_BOUND ( 'NONE', #121639, .T. ) ;
#31561=LINE ( 'NONE', #18498, #60416 ) ;
#31563=DIRECTION ( 'NONE',  ( -0.7071067811865486830, -0.7071067811865464625, -0.000000000000000000 ) ) ;
#31564=AXIS2_PLACEMENT_3D ( 'NONE', #8691, #116070, #118930 ) ;
#31565=LINE ( 'NONE', #22090, #78366 ) ;
#31566=ADVANCED_FACE ( 'NONE', ( #86702 ), #39637, .F. ) ;
#31568=CARTESIAN_POINT ( 'NONE',  ( -1.734723475976807094E-15, 13.93112307739203715, 4.000000000000000000 ) ) ;
#31569=CARTESIAN_POINT ( 'NONE',  ( 0.4892135623730947680, -27.52281430457055578, 5.000000000000000000 ) ) ;
#31570=CARTESIAN_POINT ( 'NONE',  ( -13.71003237941630104, 5.842153316012715258, 5.000000000000000000 ) ) ;
#31571=DIRECTION ( 'NONE',  ( 0.3543493200069162685, -0.000000000000000000, -0.9351131265310288487 ) ) ;
#31573=LINE ( 'NONE', #108362, #2422 ) ;
#31574=ORIENTED_EDGE ( 'NONE', *, *, #122229, .F. ) ;
#31575=DIRECTION ( 'NONE',  ( -0.6830127018922180770, -0.6830127018922204085, -0.2588190451025213501 ) ) ;
#31576=PLANE ( 'NONE',  #10530 ) ;
#31579=CARTESIAN_POINT ( 'NONE',  ( 39.18398860626899705, 28.73617430169814568, 5.000000000000000000 ) ) ;
#31580=ORIENTED_EDGE ( 'NONE', *, *, #126471, .T. ) ;
#31581=EDGE_CURVE ( 'NONE', #87749, #12285, #96113, .T. ) ;
#31582=DIRECTION ( 'NONE',  ( -0.7071067811865486830, -0.7071067811865464625, 0.000000000000000000 ) ) ;
#31584=LINE ( 'NONE', #143189, #122758 ) ;
#31586=ORIENTED_EDGE ( 'NONE', *, *, #73150, .T. ) ;
#31587=ORIENTED_EDGE ( 'NONE', *, *, #48955, .T. ) ;
#31588=CARTESIAN_POINT ( 'NONE',  ( 14.99999999999989519, 20.70535890316562444, 1.956823837851882297 ) ) ;
#31589=LINE ( 'NONE', #41027, #111609 ) ;
#31590=CARTESIAN_POINT ( 'NONE',  ( -29.29289321881324426, 20.25929247661551713, 5.000000000000000000 ) ) ;
#31592=FACE_OUTER_BOUND ( 'NONE', #19694, .T. ) ;
#31594=DIRECTION ( 'NONE',  ( 0.3543493200069162685, -0.000000000000000000, -0.9351131265310288487 ) ) ;
#31595=VECTOR ( 'NONE', #73095, 1000.000000000000000 ) ;
#31596=LINE ( 'NONE', #142506, #13616 ) ;
#31598=DIRECTION ( 'NONE',  ( -0.7071067811865486830, -0.7071067811865464625, -0.000000000000000000 ) ) ;
#31599=CARTESIAN_POINT ( 'NONE',  ( 3.183988606268992161, 28.73617430169789699, 5.000000000000000000 ) ) ;
#31600=DIRECTION ( 'NONE',  ( -0.000000000000000000, 1.000000000000000000, -0.000000000000000000 ) ) ;
#31601=ADVANCED_FACE ( 'NONE', ( #106255 ), #6928, .T. ) ;
#31602=VECTOR ( 'NONE', #133087, 1000.000000000000000 ) ;
#31603=ORIENTED_EDGE ( 'NONE', *, *, #25455, .T. ) ;
#31604=CARTESIAN_POINT ( 'NONE',  ( 11.99999999999991651, -21.84840872380823384, 2.849755605029635763 ) ) ;
#31605=VERTEX_POINT ( 'NONE', #110547 ) ;
#31610=DIRECTION ( 'NONE',  ( -0.000000000000000000, 0.3543493200069153248, 0.9351131265310292928 ) ) ;
#31611=EDGE_LOOP ( 'NONE', ( #113018, #91438, #46919, #21385 ) ) ;
#31613=DIRECTION ( 'NONE',  ( 0.7071067811865487940, 0.7071067811865463515, 0.000000000000000000 ) ) ;
#31614=CARTESIAN_POINT ( 'NONE',  ( 25.49999999999983658, 1.087461875839234038, 4.000000000000000000 ) ) ;
#31615=PLANE ( 'NONE',  #94859 ) ;
#31616=DIRECTION ( 'NONE',  ( -0.7071067811865486830, -0.7071067811865464625, 0.000000000000000000 ) ) ;
#31617=ORIENTED_EDGE ( 'NONE', *, *, #78578, .T. ) ;
#31618=FACE_OUTER_BOUND ( 'NONE', #90644, .T. ) ;
#31619=CARTESIAN_POINT ( 'NONE',  ( 5.588385094051650626, 22.22500000000000497, 4.777194822843813249 ) ) ;
#31620=PLANE ( 'NONE',  #77260 ) ;
#31621=CARTESIAN_POINT ( 'NONE',  ( 51.29974487139158867, -27.71228299555242103, 4.000000000000000000 ) ) ;
#31622=EDGE_LOOP ( 'NONE', ( #101616, #104554, #66695, #64591 ) ) ;
#31623=EDGE_CURVE ( 'NONE', #17366, #109623, #101115, .T. ) ;
#31625=VERTEX_POINT ( 'NONE', #98284 ) ;
#31627=ORIENTED_EDGE ( 'NONE', *, *, #13014, .T. ) ;
#31628=AXIS2_PLACEMENT_3D ( 'NONE', #86916, #129682, #120204 ) ;
#31629=LINE ( 'NONE', #75161, #123947 ) ;
#31630=CARTESIAN_POINT ( 'NONE',  ( -5.999999999999956479, -0.2811185226894372113, -5.995736974527501317 ) ) ;
#31631=VECTOR ( 'NONE', #74941, 1000.000000000000000 ) ;
#31632=PLANE ( 'NONE',  #131419 ) ;
#31633=LINE ( 'NONE', #30930, #47911 ) ;
#31634=ORIENTED_EDGE ( 'NONE', *, *, #124940, .F. ) ;
#31635=LINE ( 'NONE', #141083, #46935 ) ;
#31636=CARTESIAN_POINT ( 'NONE',  ( -33.29974487139158867, -27.71228299555229313, 4.000000000000000000 ) ) ;
#31637=EDGE_LOOP ( 'NONE', ( #120709, #76788, #46091, #67187 ) ) ;
#31638=VECTOR ( 'NONE', #9890, 1000.000000000000000 ) ;
#31639=ADVANCED_FACE ( 'NONE', ( #33759 ), #43196, .F. ) ;
#31640=CARTESIAN_POINT ( 'NONE',  ( -75.18398860626899705, 28.73617430169839793, 5.000000000000000000 ) ) ;
#31641=DIRECTION ( 'NONE',  ( -0.6830127018922181881, 0.6830127018922202975, -0.2588190451025214056 ) ) ;
#31642=CARTESIAN_POINT ( 'NONE',  ( -39.18398860626899705, 28.73617430169814568, 5.000000000000000000 ) ) ;
#31643=ORIENTED_EDGE ( 'NONE', *, *, #26858, .T. ) ;
#31645=AXIS2_PLACEMENT_3D ( 'NONE', #120564, #10394, #85113 ) ;
#31646=EDGE_CURVE ( 'NONE', #73943, #123539, #67083, .T. ) ;
#31647=FACE_BOUND ( 'NONE', #73290, .T. ) ;
#31648=CARTESIAN_POINT ( 'NONE',  ( 54.48921356237310221, -27.52281430457093236, 5.000000000000000000 ) ) ;
#31649=CARTESIAN_POINT ( 'NONE',  ( -71.99451991528749772, 28.92564299267988304, 4.000000000000000000 ) ) ;
#31650=PLANE ( 'NONE',  #55231 ) ;
#31651=DIRECTION ( 'NONE',  ( -0.7071067811865486830, -0.7071067811865464625, 0.000000000000000000 ) ) ;
#31652=VECTOR ( 'NONE', #136107, 1000.000000000000000 ) ;
#31653=VECTOR ( 'NONE', #84273, 1000.000000000000000 ) ;
#31656=VECTOR ( 'NONE', #26966, 1000.000000000000000 ) ;
#31657=ORIENTED_EDGE ( 'NONE', *, *, #92233, .F. ) ;
#31659=ORIENTED_EDGE ( 'NONE', *, *, #68731, .T. ) ;
#31660=ADVANCED_FACE ( 'NONE', ( #88849 ), #122145, .T. ) ;
#31661=ORIENTED_EDGE ( 'NONE', *, *, #97716, .T. ) ;
#31664=DIRECTION ( 'NONE',  ( 0.7071067811865486830, -0.7071067811865464625, -0.000000000000000000 ) ) ;
#31665=FACE_OUTER_BOUND ( 'NONE', #4812, .T. ) ;
#31666=ORIENTED_EDGE ( 'NONE', *, *, #8281, .T. ) ;
#31667=PLANE ( 'NONE',  #38968 ) ;
#31668=CARTESIAN_POINT ( 'NONE',  ( -57.29974487139158157, -27.71228299555246011, 4.000000000000000000 ) ) ;
#31669=EDGE_CURVE ( 'NONE', #30172, #81904, #21433, .T. ) ;
#31671=LINE ( 'NONE', #110619, #38845 ) ;
#31672=FACE_OUTER_BOUND ( 'NONE', #25370, .T. ) ;
#31674=ORIENTED_EDGE ( 'NONE', *, *, #42391, .T. ) ;
#31675=PLANE ( 'NONE',  #35699 ) ;
#31677=ORIENTED_EDGE ( 'NONE', *, *, #75234, .F. ) ;
#31678=EDGE_CURVE ( 'NONE', #5588, #122297, #119984, .T. ) ;
#31679=ORIENTED_EDGE ( 'NONE', *, *, #96963, .F. ) ;
#31680=EDGE_CURVE ( 'NONE', #26993, #41501, #44655, .T. ) ;
#31681=VERTEX_POINT ( 'NONE', #56246 ) ;
#31683=VERTEX_POINT ( 'NONE', #56943 ) ;
#31684=PLANE ( 'NONE',  #53598 ) ;
#31687=DIRECTION ( 'NONE',  ( -0.7071067811865486830, -0.7071067811865464625, -0.000000000000000000 ) ) ;
#31689=ORIENTED_EDGE ( 'NONE', *, *, #94742, .T. ) ;
#31690=CARTESIAN_POINT ( 'NONE',  ( -16.17183060077636370, -5.240707523384225297, 4.000000000000000000 ) ) ;
#31691=VECTOR ( 'NONE', #22482, 1000.000000000000114 ) ;
#31692=PLANE ( 'NONE',  #26157 ) ;
#31693=ADVANCED_FACE ( 'NONE', ( #88118 ), #1073, .F. ) ;
#31694=CARTESIAN_POINT ( 'NONE',  ( 42.18398860626899705, 28.73617430169816700, 5.000000000000000000 ) ) ;
#31695=CARTESIAN_POINT ( 'NONE',  ( -14.99999999999988987, -9.412538124160658271, 4.000000000000000000 ) ) ;
#31696=ORIENTED_EDGE ( 'NONE', *, *, #31528, .T. ) ;
#31697=DIRECTION ( 'NONE',  ( 0.7071067811865487940, 0.7071067811865463515, 0.000000000000000000 ) ) ;
#31698=EDGE_LOOP ( 'NONE', ( #28713, #38110, #141387, #73461 ) ) ;
#31699=ORIENTED_EDGE ( 'NONE', *, *, #136759, .F. ) ;
#31702=VECTOR ( 'NONE', #11752, 1000.000000000000000 ) ;
#31703=EDGE_LOOP ( 'NONE', ( #129102, #24569, #74600, #38447 ) ) ;
#31704=CARTESIAN_POINT ( 'NONE',  ( 11.70025512860841133, -27.71228299555198049, 4.000000000000000000 ) ) ;
#31705=VECTOR ( 'NONE', #72715, 1000.000000000000227 ) ;
#31706=DIRECTION ( 'NONE',  ( -0.7071067811865486830, -0.7071067811865464625, 0.000000000000000000 ) ) ;
#31707=VERTEX_POINT ( 'NONE', #77272 ) ;
#31708=DIRECTION ( 'NONE',  ( 0.7071067811865487940, 0.7071067811865463515, -0.000000000000000000 ) ) ;
#31709=ORIENTED_EDGE ( 'NONE', *, *, #21860, .T. ) ;
#31710=VECTOR ( 'NONE', #88750, 1000.000000000000000 ) ;
#31712=CARTESIAN_POINT ( 'NONE',  ( -39.48921356237310221, -27.52281430457082934, 5.000000000000000000 ) ) ;
#31713=ADVANCED_FACE ( 'NONE', ( #10526 ), #121443, .F. ) ;
#31714=LINE ( 'NONE', #63656, #83061 ) ;
#31715=VECTOR ( 'NONE', #77836, 1000.000000000000000 ) ;
#31716=CARTESIAN_POINT ( 'NONE',  ( 14.99999999999989875, -13.44781430457069149, 5.000000000000000000 ) ) ;
#31717=ORIENTED_EDGE ( 'NONE', *, *, #68300, .F. ) ;
#31718=ADVANCED_FACE ( 'NONE', ( #90241 ), #99684, .F. ) ;
#31719=ORIENTED_EDGE ( 'NONE', *, *, #139242, .F. ) ;
#31720=ORIENTED_EDGE ( 'NONE', *, *, #81843, .F. ) ;
#31721=CARTESIAN_POINT ( 'NONE',  ( 11.99999999999993427, 20.58746187583903264, 4.000000000000000000 ) ) ;
#31723=LINE ( 'NONE', #64353, #132980 ) ;
#31724=DIRECTION ( 'NONE',  ( -0.7071067811865487940, 0.7071067811865463515, 0.000000000000000000 ) ) ;
#31726=EDGE_CURVE ( 'NONE', #53276, #139884, #134485, .T. ) ;
#31727=CARTESIAN_POINT ( 'NONE',  ( 0.000000000000000000, 0.000000000000000000, 5.000000000000000000 ) ) ;
#31728=PLANE ( 'NONE',  #71516 ) ;
#31730=DIRECTION ( 'NONE',  ( 0.6830127018922181881, 0.6830127018922202975, -0.2588190451025214056 ) ) ;
#31731=CARTESIAN_POINT ( 'NONE',  ( -17.99999999999987566, 15.45873954670183359, -0.03131636524290101059 ) ) ;
#31733=DIRECTION ( 'NONE',  ( -0.000000000000000000, -0.3543493200069152693, 0.9351131265310292928 ) ) ;
#31734=ORIENTED_EDGE ( 'NONE', *, *, #112311, .F. ) ;
#31735=PLANE ( 'NONE',  #42963 ) ;
#31736=ORIENTED_EDGE ( 'NONE', *, *, #70379, .F. ) ;
#31737=DIRECTION ( 'NONE',  ( -0.7071067811865486830, -0.7071067811865464625, -0.000000000000000000 ) ) ;
#31738=CARTESIAN_POINT ( 'NONE',  ( -34.42500000000001137, -12.02281430457044564, 5.000000000000000000 ) ) ;
#31741=ADVANCED_FACE ( 'NONE', ( #59782 ), #81549, .F. ) ;
#31742=ADVANCED_FACE ( 'NONE', ( #69974 ), #68530, .T. ) ;
#31743=LINE ( 'NONE', #120873, #51481 ) ;
#31746=ORIENTED_EDGE ( 'NONE', *, *, #87535, .T. ) ;
#31747=CARTESIAN_POINT ( 'NONE',  ( 16.82816939922341604, -5.240707523384228850, 4.000000000000000000 ) ) ;
#31749=AXIS2_PLACEMENT_3D ( 'NONE', #90116, #132232, #11824 ) ;
#31755=EDGE_CURVE ( 'NONE', #52226, #56014, #101839, .T. ) ;
#31756=PLANE ( 'NONE',  #16092 ) ;
#31757=FACE_OUTER_BOUND ( 'NONE', #121739, .T. ) ;
#31762=VECTOR ( 'NONE', #3076, 1000.000000000000000 ) ;
#31766=EDGE_LOOP ( 'NONE', ( #84293, #92897, #90708, #52677 ) ) ;
#31768=PLANE ( 'NONE',  #55960 ) ;
#31769=ORIENTED_EDGE ( 'NONE', *, *, #104864, .T. ) ;
#31770=DIRECTION ( 'NONE',  ( 0.7071067811865487940, 0.7071067811865463515, 0.000000000000000000 ) ) ;
#31771=CARTESIAN_POINT ( 'NONE',  ( 34.92499999999998295, -21.72500000000000142, 5.000000000000000000 ) ) ;
#31772=LINE ( 'NONE', #96270, #141324 ) ;
#31773=EDGE_CURVE ( 'NONE', #52437, #40456, #135897, .T. ) ;
#31775=ORIENTED_EDGE ( 'NONE', *, *, #35334, .T. ) ;
#31776=DIRECTION ( 'NONE',  ( 0.7071067811865487940, -0.7071067811865463515, 0.000000000000000000 ) ) ;
#31777=LINE ( 'NONE', #75994, #78895 ) ;
#31778=CARTESIAN_POINT ( 'NONE',  ( -36.48921356237310221, -27.52281430457080802, 5.000000000000000000 ) ) ;
#31780=CARTESIAN_POINT ( 'NONE',  ( -7.203449814691606612, -22.22500000000000142, 15.50473165117706031 ) ) ;
#31781=EDGE_CURVE ( 'NONE', #102270, #11869, #75972, .T. ) ;
#31782=ORIENTED_EDGE ( 'NONE', *, *, #105571, .F. ) ;
#31783=DIRECTION ( 'NONE',  ( -0.7071067811865486830, -0.7071067811865464625, 0.000000000000000000 ) ) ;
#31785=ADVANCED_FACE ( 'NONE', ( #13375 ), #57652, .F. ) ;
#31786=CARTESIAN_POINT ( 'NONE',  ( 66.29974487139159578, -27.71228299555252406, 4.000000000000000000 ) ) ;
#31787=LINE ( 'NONE', #20887, #108091 ) ;
#31789=VERTEX_POINT ( 'NONE', #114138 ) ;
#31790=EDGE_CURVE ( 'NONE', #99307, #13986, #92365, .T. ) ;
#31791=EDGE_LOOP ( 'NONE', ( #87983, #96046, #34525, #90373 ) ) ;
#31795=ORIENTED_EDGE ( 'NONE', *, *, #48712, .F. ) ;
#31798=PLANE ( 'NONE',  #138336 ) ;
#31799=ORIENTED_EDGE ( 'NONE', *, *, #106370, .F. ) ;
#31800=ADVANCED_FACE ( 'NONE', ( #60508 ), #137339, .T. ) ;
#31802=CARTESIAN_POINT ( 'NONE',  ( 11.16170612452612865, -6.740707523384212863, 16.75550250614870151 ) ) ;
#31805=ORIENTED_EDGE ( 'NONE', *, *, #127569, .F. ) ;
#31808=ORIENTED_EDGE ( 'NONE', *, *, #119278, .T. ) ;
#31809=VERTEX_POINT ( 'NONE', #93817 ) ;
#31810=AXIS2_PLACEMENT_3D ( 'NONE', #139741, #5598, #95477 ) ;
#31813=CARTESIAN_POINT ( 'NONE',  ( -29.99999999999978328, -3.412538124160721331, 4.000000000000000000 ) ) ;
#31815=DIRECTION ( 'NONE',  ( 0.7071067811865486830, -0.7071067811865464625, -0.000000000000000000 ) ) ;
#31816=FACE_OUTER_BOUND ( 'NONE', #89155, .T. ) ;
#31817=DIRECTION ( 'NONE',  ( 0.7071067811865487940, -0.7071067811865463515, 0.000000000000000000 ) ) ;
#31819=ORIENTED_EDGE ( 'NONE', *, *, #69261, .T. ) ;
#31820=VECTOR ( 'NONE', #1485, 1000.000000000000227 ) ;
#31821=ORIENTED_EDGE ( 'NONE', *, *, #62878, .F. ) ;
#31822=DIRECTION ( 'NONE',  ( 0.7071067811865486830, -0.7071067811865464625, -0.000000000000000000 ) ) ;
#31823=ORIENTED_EDGE ( 'NONE', *, *, #106962, .F. ) ;
#31824=EDGE_CURVE ( 'NONE', #81813, #111086, #25697, .T. ) ;
#31826=VECTOR ( 'NONE', #90980, 1000.000000000000000 ) ;
#31828=ORIENTED_EDGE ( 'NONE', *, *, #79321, .T. ) ;
#31829=DIRECTION ( 'NONE',  ( 1.000000000000000000, 0.000000000000000000, 0.000000000000000000 ) ) ;
#31831=LINE ( 'NONE', #42735, #131262 ) ;
#31832=FACE_OUTER_BOUND ( 'NONE', #140725, .T. ) ;
#31835=ORIENTED_EDGE ( 'NONE', *, *, #72425, .T. ) ;
#31837=AXIS2_PLACEMENT_3D ( 'NONE', #133815, #69284, #23617 ) ;
#31839=EDGE_CURVE ( 'NONE', #46544, #25800, #14823, .T. ) ;
#31841=ORIENTED_EDGE ( 'NONE', *, *, #40518, .F. ) ;
#31843=CARTESIAN_POINT ( 'NONE',  ( 8.999999999999946709, 1.552185695429156187, 5.000000000000000000 ) ) ;
#31844=ADVANCED_FACE ( 'NONE', ( #3902 ), #103947, .F. ) ;
#31845=ORIENTED_EDGE ( 'NONE', *, *, #48101, .F. ) ;
#31846=ORIENTED_EDGE ( 'NONE', *, *, #86079, .F. ) ;
#31847=AXIS2_PLACEMENT_3D ( 'NONE', #99955, #45606, #89775 ) ;
#31848=ORIENTED_EDGE ( 'NONE', *, *, #137253, .T. ) ;
#31849=AXIS2_PLACEMENT_3D ( 'NONE', #112434, #142914, #99378 ) ;
#31850=ADVANCED_FACE ( 'NONE', ( #35185 ), #48903, .F. ) ;
#31851=AXIS2_PLACEMENT_3D ( 'NONE', #114350, #4094, #15700 ) ;
#31852=LINE ( 'NONE', #109405, #118348 ) ;
#31853=CARTESIAN_POINT ( 'NONE',  ( -9.121473163371414117, -20.24070752338407431, 7.412974875817811338 ) ) ;
#31854=DIRECTION ( 'NONE',  ( 0.6830127018922181881, 0.6830127018922202975, -0.2588190451025214056 ) ) ;
#31857=FACE_OUTER_BOUND ( 'NONE', #113125, .T. ) ;
#31858=EDGE_CURVE ( 'NONE', #42811, #57178, #26428, .T. ) ;
#31861=DIRECTION ( 'NONE',  ( -0.3543493200069162685, -0.000000000000000000, -0.9351131265310288487 ) ) ;
#31862=EDGE_CURVE ( 'NONE', #119359, #132971, #126431, .T. ) ;
#31863=CARTESIAN_POINT ( 'NONE',  ( 13.49999999999990408, -11.56887692260769995, 4.000000000000000000 ) ) ;
#31864=CARTESIAN_POINT ( 'NONE',  ( 4.176659101599700108, 5.259292476615659240, 15.86257073897096781 ) ) ;
#31865=PLANE ( 'NONE',  #135221 ) ;
#31867=ORIENTED_EDGE ( 'NONE', *, *, #91764, .F. ) ;
#31868=ORIENTED_EDGE ( 'NONE', *, *, #46964, .T. ) ;
#31869=LINE ( 'NONE', #45631, #77336 ) ;
#31870=ADVANCED_FACE ( 'NONE', ( #27123 ), #124305, .F. ) ;
#31871=ORIENTED_EDGE ( 'NONE', *, *, #114816, .T. ) ;
#31872=VERTEX_POINT ( 'NONE', #107540 ) ;
#31873=FACE_OUTER_BOUND ( 'NONE', #45211, .T. ) ;
#31876=VERTEX_POINT ( 'NONE', #6053 ) ;
#31877=VECTOR ( 'NONE', #23640, 1000.000000000000000 ) ;
#31878=DIRECTION ( 'NONE',  ( 0.7071067811865487940, 0.7071067811865463515, -0.000000000000000000 ) ) ;
#31879=EDGE_CURVE ( 'NONE', #37438, #98546, #74953, .T. ) ;
#31880=EDGE_CURVE ( 'NONE', #130610, #75725, #61247, .T. ) ;
#31881=ORIENTED_EDGE ( 'NONE', *, *, #75452, .F. ) ;
#31882=CARTESIAN_POINT ( 'NONE',  ( 4.828169399223495084, 0.7592924766157104211, 4.000000000000000000 ) ) ;
#31885=ORIENTED_EDGE ( 'NONE', *, *, #41238, .F. ) ;
#31887=CARTESIAN_POINT ( 'NONE',  ( 1.499999999999987566, 16.18958161055402911, -11.56426086740811066 ) ) ;
#31888=FACE_OUTER_BOUND ( 'NONE', #38705, .T. ) ;
#31889=CARTESIAN_POINT ( 'NONE',  ( -27.51665438641025574, 22.22500000000000142, 4.500000000000000888 ) ) ;
#31890=ORIENTED_EDGE ( 'NONE', *, *, #86135, .F. ) ;
#31891=EDGE_CURVE ( 'NONE', #77128, #29743, #127147, .T. ) ;
#31892=LINE ( 'NONE', #132672, #110172 ) ;
#31893=VERTEX_POINT ( 'NONE', #18357 ) ;
#31895=VERTEX_POINT ( 'NONE', #39461 ) ;
#31896=DIRECTION ( 'NONE',  ( -0.7071067811865487940, 0.7071067811865463515, -0.000000000000000000 ) ) ;
#31897=LINE ( 'NONE', #55086, #69614 ) ;
#31898=CARTESIAN_POINT ( 'NONE',  ( 15.48921356237309510, -27.52281430457066236, 5.000000000000000000 ) ) ;
#31899=DIRECTION ( 'NONE',  ( -0.7071067811865486830, -0.7071067811865464625, 0.000000000000000000 ) ) ;
#31900=EDGE_LOOP ( 'NONE', ( #141173, #119598, #90106, #134579 ) ) ;
#31901=EDGE_CURVE ( 'NONE', #18367, #59489, #50325, .T. ) ;
#31902=EDGE_CURVE ( 'NONE', #93492, #82948, #105394, .T. ) ;
#31903=CARTESIAN_POINT ( 'NONE',  ( -11.75830541574806531, 0.7592924766157104211, 14.37146558664985285 ) ) ;
#31904=LINE ( 'NONE', #62408, #132342 ) ;
#31905=CARTESIAN_POINT ( 'NONE',  ( 57.48921356237308800, -27.52281430457095368, 5.000000000000000000 ) ) ;
#31906=VERTEX_POINT ( 'NONE', #140187 ) ;
#31907=DIRECTION ( 'NONE',  ( 0.7071067811865487940, -0.7071067811865463515, 0.000000000000000000 ) ) ;
#31908=DIRECTION ( 'NONE',  ( -0.6830127018922180770, -0.6830127018922204085, -0.2588190451025213501 ) ) ;
#31910=VERTEX_POINT ( 'NONE', #62633 ) ;
#31912=EDGE_LOOP ( 'NONE', ( #41478, #40331, #39933 ) ) ;
#31913=EDGE_CURVE ( 'NONE', #78673, #92363, #84398, .T. ) ;
#31914=ORIENTED_EDGE ( 'NONE', *, *, #61755, .T. ) ;
#31915=DIRECTION ( 'NONE',  ( -0.000000000000000000, 0.3543493200069152138, -0.9351131265310292928 ) ) ;
#31916=CARTESIAN_POINT ( 'NONE',  ( -14.20710678118643955, -17.24070752338410273, 5.000000000000000000 ) ) ;
#31917=ORIENTED_EDGE ( 'NONE', *, *, #98467, .T. ) ;
#31918=LINE ( 'NONE', #76143, #58270 ) ;
#31920=LINE ( 'NONE', #129796, #98482 ) ;
#31921=LINE ( 'NONE', #44991, #76347 ) ;
#31922=VECTOR ( 'NONE', #97438, 1000.000000000000000 ) ;
#31924=CARTESIAN_POINT ( 'NONE',  ( -54.18398860626899705, 28.73617430169825226, 5.000000000000000000 ) ) ;
#31925=FACE_OUTER_BOUND ( 'NONE', #52554, .T. ) ;
#31926=CARTESIAN_POINT ( 'NONE',  ( 15.67180000000000284, 3.174999999999997602, 1.444000000000000394 ) ) ;
#31927=LINE ( 'NONE', #55117, #54125 ) ;
#31929=PLANE ( 'NONE',  #9626 ) ;
#31930=DIRECTION ( 'NONE',  ( 0.7071067811865487940, -0.7071067811865463515, 0.000000000000000000 ) ) ;
#31931=ADVANCED_FACE ( 'NONE', ( #83689 ), #127897, .T. ) ;
#31932=DIRECTION ( 'NONE',  ( -0.7071067811865487940, 0.7071067811865463515, 0.000000000000000000 ) ) ;
#31933=CARTESIAN_POINT ( 'NONE',  ( 0.8134913539763841683, -15.74070752338412049, 8.904080028138940506 ) ) ;
#31934=ORIENTED_EDGE ( 'NONE', *, *, #74960, .F. ) ;
#31936=ORIENTED_EDGE ( 'NONE', *, *, #90049, .T. ) ;
#31938=AXIS2_PLACEMENT_3D ( 'NONE', #90058, #13197, #103098 ) ;
#31939=VERTEX_POINT ( 'NONE', #29973 ) ;
#31940=ORIENTED_EDGE ( 'NONE', *, *, #106570, .F. ) ;
#31941=ORIENTED_EDGE ( 'NONE', *, *, #38402, .T. ) ;
#31942=CARTESIAN_POINT ( 'NONE',  ( 11.99999999999991651, 8.966399257802171618, 5.000000000000000000 ) ) ;
#31944=ORIENTED_EDGE ( 'NONE', *, *, #40358, .F. ) ;
#31946=CARTESIAN_POINT ( 'NONE',  ( 25.49999999999982947, 10.08746187583913922, 4.000000000000000000 ) ) ;
#31947=CARTESIAN_POINT ( 'NONE',  ( 2.999999999999981792, -4.068876922607773672, 4.000000000000000000 ) ) ;
#31948=AXIS2_PLACEMENT_3D ( 'NONE', #67713, #134371, #114025 ) ;
#31949=DIRECTION ( 'NONE',  ( 1.000000000000000000, 0.000000000000000000, 0.000000000000000000 ) ) ;
#31950=LINE ( 'NONE', #55139, #4839 ) ;
#31951=ORIENTED_EDGE ( 'NONE', *, *, #103834, .T. ) ;
#31952=DIRECTION ( 'NONE',  ( 0.3543493200069162685, -0.000000000000000000, -0.9351131265310288487 ) ) ;
#31954=AXIS2_PLACEMENT_3D ( 'NONE', #113314, #135124, #26334 ) ;
#31955=CARTESIAN_POINT ( 'NONE',  ( -72.29974487139158157, -27.71228299555256669, 4.000000000000000000 ) ) ;
#31956=CARTESIAN_POINT ( 'NONE',  ( 2.999999999999978240, 11.96639925780213609, 5.000000000000000000 ) ) ;
#31957=CARTESIAN_POINT ( 'NONE',  ( -22.39656807105343361, -14.24070752338413648, 19.24067776001720986 ) ) ;
#31959=PLANE ( 'NONE',  #37560 ) ;
#31960=ADVANCED_FACE ( 'NONE', ( #51037 ), #28579, .F. ) ;
#31961=EDGE_CURVE ( 'NONE', #133096, #131795, #72837, .T. ) ;
#31962=ORIENTED_EDGE ( 'NONE', *, *, #15981, .T. ) ;
#31963=VERTEX_POINT ( 'NONE', #16977 ) ;
#31965=ORIENTED_EDGE ( 'NONE', *, *, #138090, .T. ) ;
#31966=CARTESIAN_POINT ( 'NONE',  ( -18.48921356237309510, -27.52281430457068367, 5.000000000000000000 ) ) ;
#31967=LINE ( 'NONE', #141445, #52481 ) ;
#31968=DIRECTION ( 'NONE',  ( -0.000000000000000000, -0.3543493200069152693, 0.9351131265310292928 ) ) ;
#31969=LINE ( 'NONE', #40715, #35373 ) ;
#31970=LINE ( 'NONE', #134150, #86003 ) ;
#31974=VERTEX_POINT ( 'NONE', #53149 ) ;
#31975=PLANE ( 'NONE',  #27725 ) ;
#31977=CARTESIAN_POINT ( 'NONE',  ( 4.499999999999967137, 15.05218569542901896, 5.000000000000000000 ) ) ;
#31978=EDGE_LOOP ( 'NONE', ( #107646, #54824, #100148, #39494 ) ) ;
#31980=VERTEX_POINT ( 'NONE', #73509 ) ;
#31981=DIRECTION ( 'NONE',  ( -0.000000000000000000, -0.000000000000000000, 1.000000000000000000 ) ) ;
#31982=LINE ( 'NONE', #140056, #129529 ) ;
#31984=VECTOR ( 'NONE', #124040, 1000.000000000000227 ) ;
#31988=ORIENTED_EDGE ( 'NONE', *, *, #49774, .F. ) ;
#31989=DIRECTION ( 'NONE',  ( -0.7071067811865486830, -0.7071067811865464625, 0.000000000000000000 ) ) ;
#31990=ORIENTED_EDGE ( 'NONE', *, *, #36450, .T. ) ;
#31991=EDGE_CURVE ( 'NONE', #91335, #129128, #117672, .T. ) ;
#31992=ORIENTED_EDGE ( 'NONE', *, *, #69206, .F. ) ;
#31993=VECTOR ( 'NONE', #21695, 1000.000000000000000 ) ;
#31994=ORIENTED_EDGE ( 'NONE', *, *, #46665, .T. ) ;
#31996=FACE_OUTER_BOUND ( 'NONE', #13981, .T. ) ;
#31997=LINE ( 'NONE', #10231, #9458 ) ;
#31999=DIRECTION ( 'NONE',  ( 0.6830127018922181881, 0.6830127018922202975, -0.2588190451025214056 ) ) ;
#32000=DIRECTION ( 'NONE',  ( 1.000000000000000000, 0.000000000000000000, 0.000000000000000000 ) ) ;
#32001=CARTESIAN_POINT ( 'NONE',  ( -11.67183060077639567, -6.740707523384219968, 4.000000000000000000 ) ) ;
#32002=ADVANCED_FACE ( 'NONE', ( #74215 ), #85789, .T. ) ;
#32003=FACE_BOUND ( 'NONE', #94734, .T. ) ;
#32004=ORIENTED_EDGE ( 'NONE', *, *, #32883, .F. ) ;
#32005=DIRECTION ( 'NONE',  ( 0.7071067811865486830, -0.7071067811865464625, -0.000000000000000000 ) ) ;
#32006=EDGE_CURVE ( 'NONE', #117128, #69078, #118407, .T. ) ;
#32008=DIRECTION ( 'NONE',  ( 0.7071067811865486830, -0.7071067811865464625, -0.000000000000000000 ) ) ;
#32009=PLANE ( 'NONE',  #127245 ) ;
#32011=CARTESIAN_POINT ( 'NONE',  ( 0.000000000000000000, 21.72500000000000142, 4.500000000000000888 ) ) ;
#32012=ORIENTED_EDGE ( 'NONE', *, *, #60602, .F. ) ;
#32013=ORIENTED_EDGE ( 'NONE', *, *, #115441, .T. ) ;
#32014=CARTESIAN_POINT ( 'NONE',  ( 12.48921356237309155, -27.52281430457064104, 5.000000000000000000 ) ) ;
#32015=ORIENTED_EDGE ( 'NONE', *, *, #107521, .F. ) ;
#32016=ADVANCED_FACE ( 'NONE', ( #112376 ), #101480, .T. ) ;
#32017=EDGE_CURVE ( 'NONE', #110484, #114963, #124668, .T. ) ;
#32019=VERTEX_POINT ( 'NONE', #34822 ) ;
#32020=VECTOR ( 'NONE', #64127, 1000.000000000000000 ) ;
#32021=DIRECTION ( 'NONE',  ( -0.6830127018922181881, 0.6830127018922202975, -0.2588190451025214056 ) ) ;
#32023=EDGE_CURVE ( 'NONE', #53028, #41122, #102226, .T. ) ;
#32024=DIRECTION ( 'NONE',  ( 0.7071067811865487940, 0.7071067811865463515, 0.000000000000000000 ) ) ;
#32025=ORIENTED_EDGE ( 'NONE', *, *, #80012, .F. ) ;
#32026=FACE_OUTER_BOUND ( 'NONE', #88600, .T. ) ;
#32028=EDGE_CURVE ( 'NONE', #122674, #31094, #57307, .T. ) ;
#32029=CARTESIAN_POINT ( 'NONE',  ( 12.48921356237309155, -27.52281430457064104, 5.000000000000000000 ) ) ;
#32030=VECTOR ( 'NONE', #35685, 999.9999999999998863 ) ;
#32032=LINE ( 'NONE', #31330, #34435 ) ;
#32033=FACE_OUTER_BOUND ( 'NONE', #93599, .T. ) ;
#32034=CARTESIAN_POINT ( 'NONE',  ( 0.000000000000000000, 0.000000000000000000, 5.000000000000000000 ) ) ;
#32035=ORIENTED_EDGE ( 'NONE', *, *, #90073, .F. ) ;
#32036=ORIENTED_EDGE ( 'NONE', *, *, #5644, .T. ) ;
#32037=ORIENTED_EDGE ( 'NONE', *, *, #96786, .F. ) ;
#32038=DIRECTION ( 'NONE',  ( -0.7071067811865486830, -0.7071067811865464625, 0.000000000000000000 ) ) ;
#32040=VECTOR ( 'NONE', #94796, 1000.000000000000000 ) ;
#32041=CARTESIAN_POINT ( 'NONE',  ( 42.29974487139158157, -27.71228299555235708, 4.000000000000000000 ) ) ;
#32042=ORIENTED_EDGE ( 'NONE', *, *, #71587, .T. ) ;
#32043=AXIS2_PLACEMENT_3D ( 'NONE', #87102, #63252, #32000 ) ;
#32044=VERTEX_POINT ( 'NONE', #69607 ) ;
#32046=LINE ( 'NONE', #120435, #15492 ) ;
#32048=DIRECTION ( 'NONE',  ( 0.6830127018922180770, -0.6830127018922204085, -0.2588190451025213501 ) ) ;
#32049=VERTEX_POINT ( 'NONE', #2878 ) ;
#32050=LINE ( 'NONE', #129942, #41731 ) ;
#32053=AXIS2_PLACEMENT_3D ( 'NONE', #126168, #137038, #90698 ) ;
#32054=LINE ( 'NONE', #32792, #100017 ) ;
#32056=DIRECTION ( 'NONE',  ( 0.7071067811865487940, 0.7071067811865463515, 0.000000000000000000 ) ) ;
#32057=ORIENTED_EDGE ( 'NONE', *, *, #19179, .F. ) ;
#32059=DIRECTION ( 'NONE',  ( 0.7071067811865486830, -0.7071067811865464625, -0.000000000000000000 ) ) ;
#32060=ADVANCED_FACE ( 'NONE', ( #25344 ), #35564, .T. ) ;
#32061=LINE ( 'NONE', #140129, #68124 ) ;
#32062=LINE ( 'NONE', #76295, #56519 ) ;
#32063=ORIENTED_EDGE ( 'NONE', *, *, #79145, .T. ) ;
#32064=VECTOR ( 'NONE', #100902, 1000.000000000000000 ) ;
#32065=CARTESIAN_POINT ( 'NONE',  ( 12.29974487139158512, -27.71228299555214747, 4.000000000000000000 ) ) ;
#32066=ORIENTED_EDGE ( 'NONE', *, *, #32071, .T. ) ;
#32068=DIRECTION ( 'NONE',  ( 0.7071067811865486830, -0.7071067811865464625, -0.000000000000000000 ) ) ;
#32069=FACE_OUTER_BOUND ( 'NONE', #56395, .T. ) ;
#32070=ORIENTED_EDGE ( 'NONE', *, *, #137943, .T. ) ;
#32071=EDGE_CURVE ( 'NONE', #28105, #107272, #75648, .T. ) ;
#32072=VECTOR ( 'NONE', #111629, 1000.000000000000000 ) ;
#32073=ADVANCED_FACE ( 'NONE', ( #67469 ), #119820, .F. ) ;
#32074=CARTESIAN_POINT ( 'NONE',  ( 33.48921356237309510, -27.52281430457078670, 5.000000000000000000 ) ) ;
#32076=LINE ( 'NONE', #21193, #29969 ) ;
#32077=EDGE_CURVE ( 'NONE', #94490, #123567, #131454, .T. ) ;
#32078=CARTESIAN_POINT ( 'NONE',  ( -23.67183060077630685, 11.25929247661559884, 4.000000000000000000 ) ) ;
#32079=VECTOR ( 'NONE', #31041, 1000.000000000000000 ) ;
#32080=EDGE_CURVE ( 'NONE', #90720, #11113, #108947, .T. ) ;
#32081=ORIENTED_EDGE ( 'NONE', *, *, #66902, .F. ) ;
#32082=VECTOR ( 'NONE', #53627, 1000.000000000000000 ) ;
#32083=FACE_OUTER_BOUND ( 'NONE', #49987, .T. ) ;
#32084=DIRECTION ( 'NONE',  ( 2.781805975412905274E-17, -0.3543493200069152138, 0.9351131265310292928 ) ) ;
#32085=EDGE_LOOP ( 'NONE', ( #107349, #66560, #38828, #120370 ) ) ;
#32086=EDGE_LOOP ( 'NONE', ( #118639, #119077, #3363, #19241 ) ) ;
#32087=CARTESIAN_POINT ( 'NONE',  ( -31.49999999999977973, 18.05218569542898521, 5.000000000000000000 ) ) ;
#32088=CARTESIAN_POINT ( 'NONE',  ( -22.49999999999984013, 10.46639925780215208, 5.000000000000000000 ) ) ;
#32089=ORIENTED_EDGE ( 'NONE', *, *, #19935, .F. ) ;
#32090=LINE ( 'NONE', #54575, #112987 ) ;
#32091=CARTESIAN_POINT ( 'NONE',  ( 6.707106781186501721, 2.259292476615694323, 5.000000000000000000 ) ) ;
#32093=ORIENTED_EDGE ( 'NONE', *, *, #120742, .T. ) ;
#32094=EDGE_CURVE ( 'NONE', #34100, #43661, #7358, .T. ) ;
#32095=DIRECTION ( 'NONE',  ( -0.6830127018922180770, -0.6830127018922204085, -0.2588190451025213501 ) ) ;
#32096=CARTESIAN_POINT ( 'NONE',  ( -22.49999999999983302, -17.94781430457063820, 5.000000000000000000 ) ) ;
#32097=DIRECTION ( 'NONE',  ( 0.7071067811865486830, -0.7071067811865464625, -0.000000000000000000 ) ) ;
#32098=VECTOR ( 'NONE', #37424, 1000.000000000000227 ) ;
#32099=LINE ( 'NONE', #66172, #39031 ) ;
#32102=EDGE_LOOP ( 'NONE', ( #85745, #27588, #7246, #3780 ) ) ;
#32103=VERTEX_POINT ( 'NONE', #12328 ) ;
#32105=EDGE_CURVE ( 'NONE', #139444, #114640, #100778, .T. ) ;
#32106=ORIENTED_EDGE ( 'NONE', *, *, #29253, .T. ) ;
#32107=EDGE_LOOP ( 'NONE', ( #27687, #74232, #123213, #54892 ) ) ;
#32108=CARTESIAN_POINT ( 'NONE',  ( 19.05000000000000071, 3.174999999999997158, 4.000000000000000000 ) ) ;
#32109=FACE_OUTER_BOUND ( 'NONE', #97837, .T. ) ;
#32110=ORIENTED_EDGE ( 'NONE', *, *, #91077, .F. ) ;
#32111=PLANE ( 'NONE',  #141124 ) ;
#32112=LINE ( 'NONE', #85767, #60522 ) ;
#32113=PLANE ( 'NONE',  #39463 ) ;
#32114=EDGE_CURVE ( 'NONE', #105061, #140051, #89888, .T. ) ;
#32115=DIRECTION ( 'NONE',  ( 0.7071067811865487940, -0.7071067811865463515, 0.000000000000000000 ) ) ;
#32117=VERTEX_POINT ( 'NONE', #79067 ) ;
#32118=CARTESIAN_POINT ( 'NONE',  ( 18.18398860626898994, 28.73617430169800002, 5.000000000000000000 ) ) ;
#32119=LINE ( 'NONE', #76345, #74684 ) ;
#32120=LINE ( 'NONE', #18346, #19508 ) ;
#32121=CARTESIAN_POINT ( 'NONE',  ( 15.18398860626900237, 28.73617430169797871, 5.000000000000000000 ) ) ;
#32125=CARTESIAN_POINT ( 'NONE',  ( 34.92499999999998295, -21.72500000000000142, 5.000000000000000000 ) ) ;
#32126=FACE_OUTER_BOUND ( 'NONE', #48259, .T. ) ;
#32127=ORIENTED_EDGE ( 'NONE', *, *, #117510, .T. ) ;
#32128=VERTEX_POINT ( 'NONE', #134868 ) ;
#32130=LINE ( 'NONE', #141616, #139641 ) ;
#32131=DIRECTION ( 'NONE',  ( 0.6830127018922181881, 0.6830127018922202975, -0.2588190451025214056 ) ) ;
#32132=LINE ( 'NONE', #174, #13713 ) ;
#32133=ORIENTED_EDGE ( 'NONE', *, *, #72187, .T. ) ;
#32134=DIRECTION ( 'NONE',  ( 0.7071067811865487940, 0.7071067811865463515, 0.000000000000000000 ) ) ;
#32135=FACE_OUTER_BOUND ( 'NONE', #90230, .T. ) ;
#32136=EDGE_CURVE ( 'NONE', #77708, #107149, #32130, .T. ) ;
#32140=DIRECTION ( 'NONE',  ( 0.7071067811865487940, 0.7071067811865463515, 0.000000000000000000 ) ) ;
#32141=ORIENTED_EDGE ( 'NONE', *, *, #42234, .F. ) ;
#32143=DIRECTION ( 'NONE',  ( 0.6830127018922181881, 0.6830127018922202975, -0.2588190451025214056 ) ) ;
#32144=VECTOR ( 'NONE', #53221, 1000.000000000000227 ) ;
#32145=VECTOR ( 'NONE', #38854, 1000.000000000000000 ) ;
#32146=VECTOR ( 'NONE', #134921, 1000.000000000000000 ) ;
#32148=CARTESIAN_POINT ( 'NONE',  ( -30.48921356237309510, -27.52281430457076894, 5.000000000000000000 ) ) ;
#32149=VECTOR ( 'NONE', #91401, 1000.000000000000000 ) ;
#32150=CARTESIAN_POINT ( 'NONE',  ( 29.20710678118633652, -14.24070752338414181, 5.000000000000000000 ) ) ;
#32151=ORIENTED_EDGE ( 'NONE', *, *, #87078, .F. ) ;
#32152=EDGE_CURVE ( 'NONE', #25969, #10888, #42319, .T. ) ;
#32154=ORIENTED_EDGE ( 'NONE', *, *, #105710, .F. ) ;
#32158=CARTESIAN_POINT ( 'NONE',  ( 16.49999999999988276, -9.462702396500995761, -9.474982329943555825 ) ) ;
#32159=LINE ( 'NONE', #77814, #11300 ) ;
#32160=VECTOR ( 'NONE', #37314, 1000.000000000000000 ) ;
#32161=EDGE_LOOP ( 'NONE', ( #904, #100903, #95771, #143289 ) ) ;
#32162=CYLINDRICAL_SURFACE ( 'NONE', #43025, 5.968999999999998529 ) ;
#32164=FACE_OUTER_BOUND ( 'NONE', #127116, .T. ) ;
#32166=DIRECTION ( 'NONE',  ( 0.3543493200069162685, -0.000000000000000000, -0.9351131265310288487 ) ) ;
#32167=LINE ( 'NONE', #132944, #34034 ) ;
#32168=ORIENTED_EDGE ( 'NONE', *, *, #130652, .F. ) ;
#32169=VERTEX_POINT ( 'NONE', #24636 ) ;
#32170=AXIS2_PLACEMENT_3D ( 'NONE', #116774, #105873, #70476 ) ;
#32171=AXIS2_PLACEMENT_3D ( 'NONE', #74218, #51042, #117674 ) ;
#32176=CARTESIAN_POINT ( 'NONE',  ( 17.81601139373099940, 28.73617430169775133, 5.000000000000000000 ) ) ;
#32177=ORIENTED_EDGE ( 'NONE', *, *, #93592, .T. ) ;
#32178=FACE_OUTER_BOUND ( 'NONE', #45309, .T. ) ;
#32179=DIRECTION ( 'NONE',  ( -0.7071067811865487940, 0.7071067811865463515, 0.000000000000000000 ) ) ;
#32180=EDGE_CURVE ( 'NONE', #13816, #49354, #66668, .T. ) ;
#32181=VECTOR ( 'NONE', #30916, 1000.000000000000000 ) ;
#32183=PLANE ( 'NONE',  #41897 ) ;
#32184=VECTOR ( 'NONE', #28725, 1000.000000000000000 ) ;
#32185=FACE_BOUND ( 'NONE', #140548, .T. ) ;
#32187=ADVANCED_FACE ( 'NONE', ( #135563 ), #81183, .F. ) ;
#32188=LINE ( 'NONE', #43081, #106823 ) ;
#32189=CARTESIAN_POINT ( 'NONE',  ( 2.442822804234946688, -22.22500000000000142, 19.16006494309459285 ) ) ;
#32191=VERTEX_POINT ( 'NONE', #59447 ) ;
#32193=VECTOR ( 'NONE', #29688, 1000.000000000000000 ) ;
#32194=DIRECTION ( 'NONE',  ( 0.7071067811865486830, -0.7071067811865464625, -0.000000000000000000 ) ) ;
#32195=ORIENTED_EDGE ( 'NONE', *, *, #134026, .T. ) ;
#32197=EDGE_CURVE ( 'NONE', #143191, #47477, #70340, .T. ) ;
#32198=ORIENTED_EDGE ( 'NONE', *, *, #118453, .F. ) ;
#32200=VERTEX_POINT ( 'NONE', #127519 ) ;
#32201=ADVANCED_FACE ( 'NONE', ( #49979 ), #84053, .F. ) ;
#32203=ADVANCED_FACE ( 'NONE', ( #28924 ), #4241, .T. ) ;
#32204=ORIENTED_EDGE ( 'NONE', *, *, #92887, .T. ) ;
#32206=VECTOR ( 'NONE', #97795, 1000.000000000000000 ) ;
#32207=ADVANCED_FACE ( 'NONE', ( #115176 ), #94162, .F. ) ;
#32208=LINE ( 'NONE', #119196, #37896 ) ;
#32210=EDGE_CURVE ( 'NONE', #111562, #37040, #116640, .T. ) ;
#32212=CARTESIAN_POINT ( 'NONE',  ( -19.49999999999986500, -14.70932175296479549, -11.46312253303832840 ) ) ;
#32214=DIRECTION ( 'NONE',  ( 0.7071067811865487940, 0.7071067811865463515, 0.000000000000000000 ) ) ;
#32215=PLANE ( 'NONE',  #67130 ) ;
#32218=VERTEX_POINT ( 'NONE', #115895 ) ;
#32220=CARTESIAN_POINT ( 'NONE',  ( 7.001930566820925961, -22.22500000000000142, 4.500000000000000888 ) ) ;
#32221=EDGE_CURVE ( 'NONE', #101064, #71067, #17325, .T. ) ;
#32222=VERTEX_POINT ( 'NONE', #27473 ) ;
#32225=ORIENTED_EDGE ( 'NONE', *, *, #33764, .F. ) ;
#32226=LINE ( 'NONE', #65608, #81068 ) ;
#32227=ADVANCED_FACE ( 'NONE', ( #15852 ), #37682, .T. ) ;
#32231=ORIENTED_EDGE ( 'NONE', *, *, #35765, .F. ) ;
#32233=ORIENTED_EDGE ( 'NONE', *, *, #86515, .T. ) ;
#32234=DIRECTION ( 'NONE',  ( 0.000000000000000000, 0.3543493200069153248, 0.9351131265310291818 ) ) ;
#32235=DIRECTION ( 'NONE',  ( 0.7071067811865487940, 0.7071067811865463515, 0.000000000000000000 ) ) ;
#32237=ORIENTED_EDGE ( 'NONE', *, *, #36274, .T. ) ;
#32238=EDGE_LOOP ( 'NONE', ( #59879, #52037, #114555, #26943 ) ) ;
#32239=CARTESIAN_POINT ( 'NONE',  ( 5.671830600776432973, 8.259292476615636147, 4.000000000000000000 ) ) ;
#32240=CARTESIAN_POINT ( 'NONE',  ( 2.999999999999978240, -3.485240976185077777, -4.108735105802389320 ) ) ;
#32241=CARTESIAN_POINT ( 'NONE',  ( -2.999999999999975131, -3.412538124160726660, 4.000000000000000000 ) ) ;
#32242=ORIENTED_EDGE ( 'NONE', *, *, #63225, .T. ) ;
#32243=LINE ( 'NONE', #85901, #96679 ) ;
#32244=ORIENTED_EDGE ( 'NONE', *, *, #13956, .T. ) ;
#32245=ORIENTED_EDGE ( 'NONE', *, *, #131407, .F. ) ;
#32246=ORIENTED_EDGE ( 'NONE', *, *, #125707, .T. ) ;
#32247=ADVANCED_FACE ( 'NONE', ( #105735 ), #104314, .T. ) ;
#32249=CARTESIAN_POINT ( 'NONE',  ( -9.183988606268997046, 28.73617430169793607, 5.000000000000000000 ) ) ;
#32251=VECTOR ( 'NONE', #35870, 1000.000000000000000 ) ;
#32252=VECTOR ( 'NONE', #25000, 1000.000000000000000 ) ;
#32253=FACE_OUTER_BOUND ( 'NONE', #50929, .T. ) ;
#32254=DIRECTION ( 'NONE',  ( 0.7071067811865487940, -0.7071067811865463515, 0.000000000000000000 ) ) ;
#32255=( BOUNDED_CURVE ( )  B_SPLINE_CURVE ( 3, ( #2364, #58984, #80695, #23428 ),
 .UNSPECIFIED., .F., .T. ) 
 B_SPLINE_CURVE_WITH_KNOTS ( ( 4, 4 ),
 ( 2.779374508378133601, 4.199602562396782091 ),
 .UNSPECIFIED. ) 
 CURVE ( )  GEOMETRIC_REPRESENTATION_ITEM ( )  RATIONAL_B_SPLINE_CURVE ( ( 1.000000000000000000, 0.8388583629366748173, 0.8388583629366748173, 1.000000000000000000 ) ) 
 REPRESENTATION_ITEM ( '' )  );
#32256=ADVANCED_FACE ( 'NONE', ( #102926 ), #93469, .F. ) ;
#32258=VECTOR ( 'NONE', #9898, 1000.000000000000000 ) ;
#32259=CARTESIAN_POINT ( 'NONE',  ( -6.299744871391586898, -27.71228299555210484, 4.000000000000000000 ) ) ;
#32260=DIRECTION ( 'NONE',  ( -0.7071067811865486830, -0.7071067811865464625, 0.000000000000000000 ) ) ;
#32262=LINE ( 'NONE', #110497, #125343 ) ;
#32264=VECTOR ( 'NONE', #96588, 1000.000000000000000 ) ;
#32265=CARTESIAN_POINT ( 'NONE',  ( 6.792893218813411238, 6.759292476615645029, 5.000000000000000000 ) ) ;
#32268=CARTESIAN_POINT ( 'NONE',  ( -45.48921356237309510, -27.52281430457087197, 5.000000000000000000 ) ) ;
#32269=EDGE_LOOP ( 'NONE', ( #128859, #56317, #17433, #45860 ) ) ;
#32270=CARTESIAN_POINT ( 'NONE',  ( -23.99999999999982592, 20.96639925780204550, 5.000000000000000000 ) ) ;
#32271=CARTESIAN_POINT ( 'NONE',  ( 20.99999999999986500, 14.87792677143811026, -11.06722581663435356 ) ) ;
#32272=CARTESIAN_POINT ( 'NONE',  ( 9.707106781186480404, 17.25929247661554911, 5.000000000000000000 ) ) ;
#32274=ORIENTED_EDGE ( 'NONE', *, *, #3520, .T. ) ;
#32275=EDGE_CURVE ( 'NONE', #46867, #120251, #15166, .T. ) ;
#32277=DIRECTION ( 'NONE',  ( -1.000000000000000000, 0.000000000000000000, 0.000000000000000000 ) ) ;
#32278=DIRECTION ( 'NONE',  ( 0.7071067811865487940, -0.7071067811865463515, 0.000000000000000000 ) ) ;
#32279=AXIS2_PLACEMENT_3D ( 'NONE', #43722, #67655, #142341 ) ;
#32281=LINE ( 'NONE', #89502, #13440 ) ;
#32283=CARTESIAN_POINT ( 'NONE',  ( 7.171830600776424092, -20.24070752338407431, 4.000000000000000000 ) ) ;
#32284=AXIS2_PLACEMENT_3D ( 'NONE', #68368, #78495, #21956 ) ;
#32285=DIRECTION ( 'NONE',  ( -0.000000000000000000, -0.3543493200069152693, 0.9351131265310292928 ) ) ;
#32286=DIRECTION ( 'NONE',  ( 0.7071067811865487940, 0.7071067811865463515, 0.000000000000000000 ) ) ;
#32288=VERTEX_POINT ( 'NONE', #38378 ) ;
#32289=LINE ( 'NONE', #76521, #83512 ) ;
#32291=CARTESIAN_POINT ( 'NONE',  ( 12.32816939922343913, -6.740707523384219968, 4.000000000000000000 ) ) ;
#32292=ORIENTED_EDGE ( 'NONE', *, *, #100702, .F. ) ;
#32293=VECTOR ( 'NONE', #118257, 999.9999999999998863 ) ;
#32294=VECTOR ( 'NONE', #61393, 1000.000000000000000 ) ;
#32295=VECTOR ( 'NONE', #66009, 1000.000000000000000 ) ;
#32296=CARTESIAN_POINT ( 'NONE',  ( -3.469446951953614189E-15, -13.06887692260767864, 4.000000000000000000 ) ) ;
#32297=CARTESIAN_POINT ( 'NONE',  ( -30.81323691877862458, -22.22500000000000142, 6.558100737250206258 ) ) ;
#32299=DIRECTION ( 'NONE',  ( -0.7071067811865486830, -0.7071067811865464625, 0.000000000000000000 ) ) ;
#32301=EDGE_CURVE ( 'NONE', #121901, #38643, #7122, .T. ) ;
#32302=ORIENTED_EDGE ( 'NONE', *, *, #141353, .F. ) ;
#32304=EDGE_LOOP ( 'NONE', ( #3719, #75236, #61506, #92929 ) ) ;
#32305=CARTESIAN_POINT ( 'NONE',  ( 24.48921356237309510, -27.52281430457072631, 5.000000000000000000 ) ) ;
#32306=CARTESIAN_POINT ( 'NONE',  ( -36.48921356237310221, -27.52281430457080802, 5.000000000000000000 ) ) ;
#32307=VECTOR ( 'NONE', #115694, 1000.000000000000000 ) ;
#32308=AXIS2_PLACEMENT_3D ( 'NONE', #66134, #66833, #89292 ) ;
#32309=LINE ( 'NONE', #54779, #93618 ) ;
#32312=DIRECTION ( 'NONE',  ( -0.7071067811865487940, 0.7071067811865463515, 0.000000000000000000 ) ) ;
#32313=DIRECTION ( 'NONE',  ( -0.7071067811865487940, 0.7071067811865463515, 0.000000000000000000 ) ) ;
#32314=ORIENTED_EDGE ( 'NONE', *, *, #48558, .T. ) ;
#32316=CARTESIAN_POINT ( 'NONE',  ( -65.99451991528749772, 28.92564299267984396, 4.000000000000000000 ) ) ;
#32317=CARTESIAN_POINT ( 'NONE',  ( 42.48921356237308800, -27.52281430457085065, 5.000000000000000000 ) ) ;
#32320=ORIENTED_EDGE ( 'NONE', *, *, #135915, .F. ) ;
#32321=DIRECTION ( 'NONE',  ( 1.000000000000000000, 0.000000000000000000, 0.000000000000000000 ) ) ;
#32322=ORIENTED_EDGE ( 'NONE', *, *, #142994, .F. ) ;
#32323=ADVANCED_FACE ( 'NONE', ( #98457 ), #118773, .T. ) ;
#32325=FACE_OUTER_BOUND ( 'NONE', #7197, .T. ) ;
#32326=ORIENTED_EDGE ( 'NONE', *, *, #136662, .F. ) ;
#32328=CARTESIAN_POINT ( 'NONE',  ( 0.000000000000000000, 0.000000000000000000, 5.000000000000000000 ) ) ;
#32329=DIRECTION ( 'NONE',  ( 1.000000000000000000, 0.000000000000000000, 0.000000000000000000 ) ) ;
#32330=CARTESIAN_POINT ( 'NONE',  ( -8.999999999999934275, 1.552185695429156187, 5.000000000000000000 ) ) ;
#32331=EDGE_CURVE ( 'NONE', #108896, #33283, #129647, .T. ) ;
#32333=CARTESIAN_POINT ( 'NONE',  ( 34.42499999999998295, -3.022814304570575761, 5.000000000000000000 ) ) ;
#32334=EDGE_LOOP ( 'NONE', ( #44962, #90749, #134060, #36809 ) ) ;
#32335=DIRECTION ( 'NONE',  ( -0.6830127018922180770, -0.6830127018922204085, -0.2588190451025213501 ) ) ;
#32337=DIRECTION ( 'NONE',  ( 0.3543493200069162685, -0.000000000000000000, -0.9351131265310288487 ) ) ;
#32338=DIRECTION ( 'NONE',  ( -0.7071067811865487940, 0.7071067811865463515, -0.000000000000000000 ) ) ;
#32339=EDGE_LOOP ( 'NONE', ( #43489, #95086, #84490, #39937 ) ) ;
#32340=EDGE_LOOP ( 'NONE', ( #109656, #24891, #136018, #110837 ) ) ;
#32342=EDGE_LOOP ( 'NONE', ( #14189, #5938, #66972, #109698 ) ) ;
#32343=LINE ( 'NONE', #109893, #3539 ) ;
#32344=CARTESIAN_POINT ( 'NONE',  ( 11.99999999999992006, -6.108550654416948333, -3.114665004254939973 ) ) ;
#32347=EDGE_LOOP ( 'NONE', ( #92425, #87650, #101324 ) ) ;
#32348=VERTEX_POINT ( 'NONE', #86880 ) ;
#32349=CARTESIAN_POINT ( 'NONE',  ( -11.99999999999991296, -9.033600742197648970, 5.000000000000000000 ) ) ;
#32351=ORIENTED_EDGE ( 'NONE', *, *, #63274, .F. ) ;
#32352=CARTESIAN_POINT ( 'NONE',  ( 1.828169399223512848, -17.24070752338410983, 4.000000000000000000 ) ) ;
#32353=DIRECTION ( 'NONE',  ( 0.7071067811865486830, -0.7071067811865464625, -0.000000000000000000 ) ) ;
#32355=VECTOR ( 'NONE', #20261, 999.9999999999998863 ) ;
#32357=VECTOR ( 'NONE', #69092, 1000.000000000000227 ) ;
#32358=ORIENTED_EDGE ( 'NONE', *, *, #132781, .F. ) ;
#32359=AXIS2_PLACEMENT_3D ( 'NONE', #94591, #60597, #82324 ) ;
#32360=FACE_BOUND ( 'NONE', #100645, .T. ) ;
#32361=LINE ( 'NONE', #63593, #8394 ) ;
#32362=CARTESIAN_POINT ( 'NONE',  ( -27.32816939922334143, 20.25929247661551003, 4.000000000000000000 ) ) ;
#32364=AXIS2_PLACEMENT_3D ( 'NONE', #136941, #37653, #71702 ) ;
#32365=LINE ( 'NONE', #86755, #59699 ) ;
#32368=ORIENTED_EDGE ( 'NONE', *, *, #8124, .F. ) ;
#32369=EDGE_CURVE ( 'NONE', #86631, #84615, #74588, .T. ) ;
#32370=VECTOR ( 'NONE', #57595, 1000.000000000000000 ) ;
#32371=ORIENTED_EDGE ( 'NONE', *, *, #34294, .T. ) ;
#32373=( BOUNDED_CURVE ( )  B_SPLINE_CURVE ( 3, ( #75391, #119564, #139238, #18101 ),
 .UNSPECIFIED., .F., .T. ) 
 B_SPLINE_CURVE_WITH_KNOTS ( ( 4, 4 ),
 ( 3.334020839929785929, 3.401188224464155585 ),
 .UNSPECIFIED. ) 
 CURVE ( )  GEOMETRIC_REPRESENTATION_ITEM ( )  RATIONAL_B_SPLINE_CURVE ( ( 1.000000000000000000, 0.9996240805387412998, 0.9996240805387412998, 1.000000000000000000 ) ) 
 REPRESENTATION_ITEM ( '' )  );
#32374=ORIENTED_EDGE ( 'NONE', *, *, #99072, .T. ) ;
#32376=EDGE_CURVE ( 'NONE', #66690, #96412, #84728, .T. ) ;
#32377=ORIENTED_EDGE ( 'NONE', *, *, #71274, .F. ) ;
#32381=DIRECTION ( 'NONE',  ( -0.7071067811865486830, -0.7071067811865464625, -0.000000000000000000 ) ) ;
#32382=VECTOR ( 'NONE', #24462, 1000.000000000000000 ) ;
#32383=PLANE ( 'NONE',  #63657 ) ;
#32384=ORIENTED_EDGE ( 'NONE', *, *, #54317, .T. ) ;
#32385=DIRECTION ( 'NONE',  ( 0.7071067811865487940, -0.7071067811865463515, 0.000000000000000000 ) ) ;
#32386=LINE ( 'NONE', #107070, #114377 ) ;
#32388=CARTESIAN_POINT ( 'NONE',  ( 0.000000000000000000, 1.931123077392161935, 4.000000000000000000 ) ) ;
#32390=VECTOR ( 'NONE', #55517, 1000.000000000000227 ) ;
#32392=ORIENTED_EDGE ( 'NONE', *, *, #29357, .T. ) ;
#32393=VECTOR ( 'NONE', #60318, 1000.000000000000000 ) ;
#32394=FACE_OUTER_BOUND ( 'NONE', #22695, .T. ) ;
#32395=DIRECTION ( 'NONE',  ( -0.7071067811865486830, 0.7071067811865464625, 0.000000000000000000 ) ) ;
#32396=VECTOR ( 'NONE', #18703, 999.9999999999998863 ) ;
#32397=EDGE_CURVE ( 'NONE', #82859, #102617, #106439, .T. ) ;
#32398=ORIENTED_EDGE ( 'NONE', *, *, #63248, .F. ) ;
#32399=ORIENTED_EDGE ( 'NONE', *, *, #132187, .F. ) ;
#32400=EDGE_CURVE ( 'NONE', #95357, #7059, #66558, .T. ) ;
#32402=ORIENTED_EDGE ( 'NONE', *, *, #85897, .T. ) ;
#32404=VECTOR ( 'NONE', #35187, 1000.000000000000000 ) ;
#32405=ORIENTED_EDGE ( 'NONE', *, *, #140232, .T. ) ;
#32411=CARTESIAN_POINT ( 'NONE',  ( 1.499999999999997780, 1.087461875839228931, 4.000000000000000000 ) ) ;
#32412=VERTEX_POINT ( 'NONE', #21620 ) ;
#32413=DIRECTION ( 'NONE',  ( 0.7071067811865487940, 0.7071067811865463515, -0.000000000000000000 ) ) ;
#32414=AXIS2_PLACEMENT_3D ( 'NONE', #13902, #59604, #136410 ) ;
#32415=DIRECTION ( 'NONE',  ( 0.6830127018922180770, -0.6830127018922204085, -0.2588190451025213501 ) ) ;
#32417=CARTESIAN_POINT ( 'NONE',  ( -2.999999999999981792, -22.22500000000000142, 4.412002311790018894 ) ) ;
#32418=ORIENTED_EDGE ( 'NONE', *, *, #45655, .F. ) ;
#32419=LINE ( 'NONE', #86802, #62284 ) ;
#32420=ORIENTED_EDGE ( 'NONE', *, *, #84429, .F. ) ;
#32421=ORIENTED_EDGE ( 'NONE', *, *, #63784, .F. ) ;
#32422=ORIENTED_EDGE ( 'NONE', *, *, #51510, .F. ) ;
#32423=EDGE_CURVE ( 'NONE', #72772, #107486, #22288, .T. ) ;
#32425=VERTEX_POINT ( 'NONE', #556 ) ;
#32426=AXIS2_PLACEMENT_3D ( 'NONE', #98029, #106008, #130675 ) ;
#32427=DIRECTION ( 'NONE',  ( -0.7071067811865486830, -0.7071067811865464625, 0.000000000000000000 ) ) ;
#32428=DIRECTION ( 'NONE',  ( -0.6830127018922181881, 0.6830127018922202975, -0.2588190451025214056 ) ) ;
#32429=ORIENTED_EDGE ( 'NONE', *, *, #117095, .F. ) ;
#32430=FACE_OUTER_BOUND ( 'NONE', #34067, .T. ) ;
#32431=ORIENTED_EDGE ( 'NONE', *, *, #140831, .F. ) ;
#32433=VECTOR ( 'NONE', #38496, 1000.000000000000000 ) ;
#32434=ADVANCED_FACE ( 'NONE', ( #79625 ), #68030, .T. ) ;
#32436=CARTESIAN_POINT ( 'NONE',  ( -28.49999999999980105, -2.947814304570797184, 5.000000000000000000 ) ) ;
#32437=CARTESIAN_POINT ( 'NONE',  ( -25.82816939922334853, 6.759292476615651246, 4.000000000000000000 ) ) ;
#32438=ORIENTED_EDGE ( 'NONE', *, *, #50749, .F. ) ;
#32439=ORIENTED_EDGE ( 'NONE', *, *, #4105, .T. ) ;
#32440=EDGE_CURVE ( 'NONE', #25852, #110079, #17076, .T. ) ;
#32441=ORIENTED_EDGE ( 'NONE', *, *, #78693, .F. ) ;
#32444=DIRECTION ( 'NONE',  ( 0.6830127018922180770, -0.6830127018922204085, -0.2588190451025213501 ) ) ;
#32445=FACE_OUTER_BOUND ( 'NONE', #20905, .T. ) ;
#32446=AXIS2_PLACEMENT_3D ( 'NONE', #8475, #32428, #31706 ) ;
#32449=ADVANCED_FACE ( 'NONE', ( #24464 ), #111471, .F. ) ;
#32450=FACE_OUTER_BOUND ( 'NONE', #82176, .T. ) ;
#32451=CARTESIAN_POINT ( 'NONE',  ( -18.48921356237309510, -27.52281430457068367, 5.000000000000000000 ) ) ;
#32452=VERTEX_POINT ( 'NONE', #54974 ) ;
#32453=LINE ( 'NONE', #20116, #27811 ) ;
#32454=VECTOR ( 'NONE', #92228, 1000.000000000000000 ) ;
#32455=VERTEX_POINT ( 'NONE', #56440 ) ;
#32456=VECTOR ( 'NONE', #39755, 1000.000000000000000 ) ;
#32457=AXIS2_PLACEMENT_3D ( 'NONE', #63143, #18134, #72612 ) ;
#32458=AXIS2_PLACEMENT_3D ( 'NONE', #126725, #94802, #69546 ) ;
#32459=LINE ( 'NONE', #68669, #70802 ) ;
#32460=ORIENTED_EDGE ( 'NONE', *, *, #116729, .T. ) ;
#32462=FACE_OUTER_BOUND ( 'NONE', #58691, .T. ) ;
#32464=ORIENTED_EDGE ( 'NONE', *, *, #123548, .F. ) ;
#32466=LINE ( 'NONE', #30311, #32981 ) ;
#32467=ORIENTED_EDGE ( 'NONE', *, *, #143247, .F. ) ;
#32468=PLANE ( 'NONE',  #94740 ) ;
#32469=ORIENTED_EDGE ( 'NONE', *, *, #140099, .T. ) ;
#32470=CARTESIAN_POINT ( 'NONE',  ( -10.67372558692450113, -22.22500000000000142, 14.18971443535745358 ) ) ;
#32471=VECTOR ( 'NONE', #38545, 1000.000000000000227 ) ;
#32473=DIRECTION ( 'NONE',  ( -0.3543493200069162685, -0.000000000000000000, -0.9351131265310288487 ) ) ;
#32475=CARTESIAN_POINT ( 'NONE',  ( 0.000000000000000000, 0.000000000000000000, 5.000000000000000000 ) ) ;
#32478=CARTESIAN_POINT ( 'NONE',  ( 23.70025512860841133, -27.71228299555189523, 4.000000000000000000 ) ) ;
#32479=CARTESIAN_POINT ( 'NONE',  ( -0.1839886062690032631, 28.73617430169787568, 5.000000000000000000 ) ) ;
#32482=VECTOR ( 'NONE', #15840, 1000.000000000000000 ) ;
#32484=CARTESIAN_POINT ( 'NONE',  ( -32.99999999999976552, 7.931123077392111753, 4.000000000000000000 ) ) ;
#32485=ORIENTED_EDGE ( 'NONE', *, *, #80089, .F. ) ;
#32486=ORIENTED_EDGE ( 'NONE', *, *, #30038, .F. ) ;
#32487=VECTOR ( 'NONE', #53170, 999.9999999999998863 ) ;
#32488=FACE_OUTER_BOUND ( 'NONE', #36456, .T. ) ;
#32490=EDGE_CURVE ( 'NONE', #83478, #64860, #12155, .T. ) ;
#32491=EDGE_CURVE ( 'NONE', #54885, #48586, #1950, .T. ) ;
#32492=VECTOR ( 'NONE', #41744, 1000.000000000000114 ) ;
#32493=FACE_OUTER_BOUND ( 'NONE', #19269, .T. ) ;
#32494=CARTESIAN_POINT ( 'NONE',  ( 78.29974487139158157, -27.71228299555260577, 4.000000000000000000 ) ) ;
#32497=ORIENTED_EDGE ( 'NONE', *, *, #137923, .F. ) ;
#32498=AXIS2_PLACEMENT_3D ( 'NONE', #126565, #70118, #36710 ) ;
#32501=DIRECTION ( 'NONE',  ( -0.6830127018922180770, -0.6830127018922204085, -0.2588190451025213501 ) ) ;
#32502=EDGE_CURVE ( 'NONE', #37517, #84503, #33934, .T. ) ;
#32504=VECTOR ( 'NONE', #18497, 1000.000000000000000 ) ;
#32505=EDGE_CURVE ( 'NONE', #84071, #85957, #44096, .T. ) ;
#32506=CARTESIAN_POINT ( 'NONE',  ( -8.999999999999934275, -3.412538124160724884, 4.000000000000000000 ) ) ;
#32507=ORIENTED_EDGE ( 'NONE', *, *, #131636, .T. ) ;
#32510=PLANE ( 'NONE',  #38696 ) ;
#32512=ORIENTED_EDGE ( 'NONE', *, *, #132380, .T. ) ;
#32513=EDGE_LOOP ( 'NONE', ( #38754, #62765, #42751, #56442 ) ) ;
#32514=ORIENTED_EDGE ( 'NONE', *, *, #127816, .T. ) ;
#32517=VERTEX_POINT ( 'NONE', #89721 ) ;
#32518=DIRECTION ( 'NONE',  ( -0.000000000000000000, -0.000000000000000000, 1.000000000000000000 ) ) ;
#32519=VECTOR ( 'NONE', #82083, 1000.000000000000227 ) ;
#32520=LINE ( 'NONE', #10034, #54733 ) ;
#32521=ORIENTED_EDGE ( 'NONE', *, *, #6738, .F. ) ;
#32523=CARTESIAN_POINT ( 'NONE',  ( 51.48921356237309510, -27.52281430457091460, 5.000000000000000000 ) ) ;
#32526=ORIENTED_EDGE ( 'NONE', *, *, #136975, .F. ) ;
#32527=CARTESIAN_POINT ( 'NONE',  ( 45.48921356237309510, -27.52281430457087197, 5.000000000000000000 ) ) ;
#32528=LINE ( 'NONE', #44880, #37919 ) ;
#32529=AXIS2_PLACEMENT_3D ( 'NONE', #30456, #85517, #29711 ) ;
#32530=ORIENTED_EDGE ( 'NONE', *, *, #62047, .T. ) ;
#32531=ORIENTED_EDGE ( 'NONE', *, *, #138091, .T. ) ;
#32532=VERTEX_POINT ( 'NONE', #33252 ) ;
#32533=PLANE ( 'NONE',  #16690 ) ;
#32534=DIRECTION ( 'NONE',  ( 0.7071067811865487940, 0.7071067811865463515, 0.000000000000000000 ) ) ;
#32535=LINE ( 'NONE', #106672, #120573 ) ;
#32536=AXIS2_PLACEMENT_3D ( 'NONE', #43704, #44452, #77773 ) ;
#32537=VECTOR ( 'NONE', #139255, 1000.000000000000000 ) ;
#32539=CARTESIAN_POINT ( 'NONE',  ( -54.48921356237310221, -27.52281430457093236, 5.000000000000000000 ) ) ;
#32541=VERTEX_POINT ( 'NONE', #93295 ) ;
#32542=EDGE_LOOP ( 'NONE', ( #81905, #132905, #26230, #116536 ) ) ;
#32543=EDGE_CURVE ( 'NONE', #130580, #4806, #103433, .T. ) ;
#32544=DIRECTION ( 'NONE',  ( -0.7071067811865486830, 0.7071067811865464625, 0.000000000000000000 ) ) ;
#32545=ORIENTED_EDGE ( 'NONE', *, *, #105621, .F. ) ;
#32548=EDGE_CURVE ( 'NONE', #89800, #36309, #4078, .T. ) ;
#32549=ADVANCED_FACE ( 'NONE', ( #38917 ), #83140, .F. ) ;
#32552=CARTESIAN_POINT ( 'NONE',  ( 20.53839644629416128, -9.740707523384177335, 17.74957260769615530 ) ) ;
#32553=EDGE_LOOP ( 'NONE', ( #77886, #45065, #128194, #120762 ) ) ;
#32554=LINE ( 'NONE', #97794, #52910 ) ;
#32555=CARTESIAN_POINT ( 'NONE',  ( -8.999999999999934275, -4.447814304570786526, 5.000000000000000000 ) ) ;
#32556=DIRECTION ( 'NONE',  ( 0.7071067811865487940, 0.7071067811865463515, 0.000000000000000000 ) ) ;
#32557=DIRECTION ( 'NONE',  ( 0.000000000000000000, -1.000000000000000000, 0.000000000000000000 ) ) ;
#32559=AXIS2_PLACEMENT_3D ( 'NONE', #33209, #65105, #86843 ) ;
#32563=EDGE_LOOP ( 'NONE', ( #96368, #78645, #37820, #26013 ) ) ;
#32564=VECTOR ( 'NONE', #61338, 1000.000000000000000 ) ;
#32565=CARTESIAN_POINT ( 'NONE',  ( 5.671830600776432973, -15.74070752338412049, 4.000000000000000000 ) ) ;
#32566=EDGE_CURVE ( 'NONE', #61026, #28815, #31516, .T. ) ;
#32567=VERTEX_POINT ( 'NONE', #71556 ) ;
#32568=CARTESIAN_POINT ( 'NONE',  ( -2.999999999999975131, -3.033600742197712030, 5.000000000000000000 ) ) ;
#32572=ORIENTED_EDGE ( 'NONE', *, *, #88186, .T. ) ;
#32573=DIRECTION ( 'NONE',  ( -0.000000000000000000, 0.3543493200069153248, 0.9351131265310292928 ) ) ;
#32575=ORIENTED_EDGE ( 'NONE', *, *, #127846, .F. ) ;
#32576=VECTOR ( 'NONE', #139315, 1000.000000000000000 ) ;
#32577=VERTEX_POINT ( 'NONE', #48363 ) ;
#32578=ADVANCED_FACE ( 'NONE', ( #102757 ), #91856, .F. ) ;
#32579=DIRECTION ( 'NONE',  ( 0.7071067811865486830, -0.7071067811865464625, -0.000000000000000000 ) ) ;
#32580=CARTESIAN_POINT ( 'NONE',  ( 20.01088028653934003, -22.02621442084248571, 4.990779571109219326 ) ) ;
#32581=PLANE ( 'NONE',  #896 ) ;
#32583=PLANE ( 'NONE',  #31197 ) ;
#32584=PLANE ( 'NONE',  #50527 ) ;
#32585=CARTESIAN_POINT ( 'NONE',  ( -16.49999999999988276, 16.77039438581777375, 0.4657186855308104723 ) ) ;
#32586=DIRECTION ( 'NONE',  ( 0.6830127018922181881, 0.6830127018922202975, -0.2588190451025214056 ) ) ;
#32587=VECTOR ( 'NONE', #81694, 1000.000000000000000 ) ;
#32588=ADVANCED_FACE ( 'NONE', ( #37508 ), #15003, .F. ) ;
#32589=CARTESIAN_POINT ( 'NONE',  ( -27.18398860626900060, 28.73617430169806042, 5.000000000000000000 ) ) ;
#32592=AXIS2_PLACEMENT_3D ( 'NONE', #44354, #32021, #58 ) ;
#32593=CARTESIAN_POINT ( 'NONE',  ( 30.81246187583926144, -22.22500000000000142, 4.000000000000000000 ) ) ;
#32594=CARTESIAN_POINT ( 'NONE',  ( -66.18398860626901126, 28.73617430169833753, 5.000000000000000000 ) ) ;
#32595=ORIENTED_EDGE ( 'NONE', *, *, #51554, .F. ) ;
#32597=ORIENTED_EDGE ( 'NONE', *, *, #89982, .T. ) ;
#32599=ORIENTED_EDGE ( 'NONE', *, *, #105243, .T. ) ;
#32600=CARTESIAN_POINT ( 'NONE',  ( 3.489213562373097322, -27.52281430457057709, 5.000000000000000000 ) ) ;
#32601=EDGE_LOOP ( 'NONE', ( #92221, #75420, #82628 ) ) ;
#32602=VECTOR ( 'NONE', #97508, 1000.000000000000000 ) ;
#32603=ORIENTED_EDGE ( 'NONE', *, *, #76930, .F. ) ;
#32604=DIRECTION ( 'NONE',  ( 0.7071067811865487940, 0.7071067811865463515, -0.000000000000000000 ) ) ;
#32605=CARTESIAN_POINT ( 'NONE',  ( 10.82816939922345156, -14.24070752338413293, 4.000000000000000000 ) ) ;
#32607=LINE ( 'NONE', #55069, #95845 ) ;
#32608=LINE ( 'NONE', #76842, #14000 ) ;
#32609=EDGE_CURVE ( 'NONE', #24642, #24958, #26611, .T. ) ;
#32610=VERTEX_POINT ( 'NONE', #15682 ) ;
#32611=EDGE_CURVE ( 'NONE', #19510, #128631, #16417, .T. ) ;
#32612=CARTESIAN_POINT ( 'NONE',  ( 32.67183060077623935, -12.74070752338415602, 4.000000000000000000 ) ) ;
#32615=AXIS2_PLACEMENT_3D ( 'NONE', #5331, #71341, #49614 ) ;
#32617=ORIENTED_EDGE ( 'NONE', *, *, #142645, .T. ) ;
#32620=FACE_OUTER_BOUND ( 'NONE', #58915, .T. ) ;
#32621=CARTESIAN_POINT ( 'NONE',  ( 35.99451991528749772, 28.92564299267963079, 4.000000000000000000 ) ) ;
#32622=ORIENTED_EDGE ( 'NONE', *, *, #7414, .F. ) ;
#32623=VERTEX_POINT ( 'NONE', #69424 ) ;
#32624=VECTOR ( 'NONE', #50846, 999.9999999999998863 ) ;
#32625=VERTEX_POINT ( 'NONE', #57593 ) ;
#32627=PLANE ( 'NONE',  #78715 ) ;
#32628=DIRECTION ( 'NONE',  ( -0.000000000000000000, -0.3543493200069152693, 0.9351131265310292928 ) ) ;
#32629=CARTESIAN_POINT ( 'NONE',  ( -15.78162688292483118, 21.74787736706805674, 4.999607392498049308 ) ) ;
#32630=PLANE ( 'NONE',  #3265 ) ;
#32632=CARTESIAN_POINT ( 'NONE',  ( 15.48921356237309510, -27.52281430457066236, 5.000000000000000000 ) ) ;
#32634=DIRECTION ( 'NONE',  ( -0.6830127018922180770, -0.6830127018922204085, -0.2588190451025213501 ) ) ;
#32635=ORIENTED_EDGE ( 'NONE', *, *, #52665, .T. ) ;
#32637=AXIS2_PLACEMENT_3D ( 'NONE', #114257, #57062, #68642 ) ;
#32638=PLANE ( 'NONE',  #84098 ) ;
#32639=ORIENTED_EDGE ( 'NONE', *, *, #35749, .F. ) ;
#32640=DIRECTION ( 'NONE',  ( -0.6830127018922180770, -0.6830127018922204085, -0.2588190451025213501 ) ) ;
#32641=ORIENTED_EDGE ( 'NONE', *, *, #36614, .F. ) ;
#32642=ORIENTED_EDGE ( 'NONE', *, *, #47023, .F. ) ;
#32643=CARTESIAN_POINT ( 'NONE',  ( 0.000000000000000000, 0.000000000000000000, 5.000000000000000000 ) ) ;
#32645=VECTOR ( 'NONE', #136411, 1000.000000000000227 ) ;
#32646=ORIENTED_EDGE ( 'NONE', *, *, #127332, .F. ) ;
#32647=CARTESIAN_POINT ( 'NONE',  ( 0.000000000000000000, 0.000000000000000000, 5.000000000000000000 ) ) ;
#32648=DIRECTION ( 'NONE',  ( -0.7071067811865486830, -0.7071067811865464625, 0.000000000000000000 ) ) ;
#32649=CARTESIAN_POINT ( 'NONE',  ( 6.299744871391586898, -27.71228299555210484, 4.000000000000000000 ) ) ;
#32650=CARTESIAN_POINT ( 'NONE',  ( 4.603431928946396745, -14.24070752338413648, 19.24067776001727026 ) ) ;
#32652=PLANE ( 'NONE',  #58432 ) ;
#32653=LINE ( 'NONE', #78296, #12364 ) ;
#32655=DIRECTION ( 'NONE',  ( 0.7071067811865487940, 0.7071067811865463515, 0.000000000000000000 ) ) ;
#32656=CARTESIAN_POINT ( 'NONE',  ( 10.49999999999992895, 16.77039438581780217, 0.4657186855307497431 ) ) ;
#32657=CARTESIAN_POINT ( 'NONE',  ( -20.67183060077632817, 14.25929247661556865, 4.000000000000000000 ) ) ;
#32659=CARTESIAN_POINT ( 'NONE',  ( -2.010880286539463935, -22.02621442084248216, 4.990779571109222879 ) ) ;
#32660=CARTESIAN_POINT ( 'NONE',  ( -18.32816939922339472, 11.25929247661559884, 4.000000000000000000 ) ) ;
#32661=EDGE_LOOP ( 'NONE', ( #66423, #75087, #43937 ) ) ;
#32662=( BOUNDED_CURVE ( )  B_SPLINE_CURVE ( 3, ( #73978, #118895, #52899, #139257 ),
 .UNSPECIFIED., .F., .F. ) 
 B_SPLINE_CURVE_WITH_KNOTS ( ( 4, 4 ),
 ( 1.208578181583235267, 1.359146454359416278 ),
 .UNSPECIFIED. ) 
 CURVE ( )  GEOMETRIC_REPRESENTATION_ITEM ( )  RATIONAL_B_SPLINE_CURVE ( ( 1.000000000000000000, 0.9981116584018958626, 0.9981116584018958626, 1.000000000000000000 ) ) 
 REPRESENTATION_ITEM ( '' )  );
#32663=ORIENTED_EDGE ( 'NONE', *, *, #58045, .T. ) ;
#32664=VECTOR ( 'NONE', #125097, 1000.000000000000000 ) ;
#32666=VECTOR ( 'NONE', #44890, 1000.000000000000000 ) ;
#32668=ORIENTED_EDGE ( 'NONE', *, *, #13493, .T. ) ;
#32669=ORIENTED_EDGE ( 'NONE', *, *, #51359, .T. ) ;
#32670=FACE_OUTER_BOUND ( 'NONE', #89409, .T. ) ;
#32671=CARTESIAN_POINT ( 'NONE',  ( 12.18398860626900060, 28.73617430169795739, 5.000000000000000000 ) ) ;
#32673=AXIS2_PLACEMENT_3D ( 'NONE', #22787, #69958, #48162 ) ;
#32674=VECTOR ( 'NONE', #45324, 1000.000000000000000 ) ;
#32676=EDGE_LOOP ( 'NONE', ( #47320, #58207, #96380, #41486 ) ) ;
#32677=( BOUNDED_CURVE ( )  B_SPLINE_CURVE ( 3, ( #65530, #109704, #143046, #79274 ),
 .UNSPECIFIED., .F., .F. ) 
 B_SPLINE_CURVE_WITH_KNOTS ( ( 4, 4 ),
 ( 5.584306267627116682, 5.657315652343092971 ),
 .UNSPECIFIED. ) 
 CURVE ( )  GEOMETRIC_REPRESENTATION_ITEM ( )  RATIONAL_B_SPLINE_CURVE ( ( 1.000000000000000000, 0.9995558518042845231, 0.9995558518042845231, 1.000000000000000000 ) ) 
 REPRESENTATION_ITEM ( '' )  );
#32679=VECTOR ( 'NONE', #77720, 1000.000000000000000 ) ;
#32680=DIRECTION ( 'NONE',  ( -0.000000000000000000, 0.3543493200069153248, 0.9351131265310292928 ) ) ;
#32682=DIRECTION ( 'NONE',  ( 0.3543493200069162685, -0.000000000000000000, -0.9351131265310288487 ) ) ;
#32683=EDGE_CURVE ( 'NONE', #98472, #52633, #133017, .T. ) ;
#32684=VERTEX_POINT ( 'NONE', #68477 ) ;
#32686=ADVANCED_FACE ( 'NONE', ( #67776 ), #24922, .T. ) ;
#32687=DIRECTION ( 'NONE',  ( -0.000000000000000000, 0.000000000000000000, 1.000000000000000000 ) ) ;
#32688=AXIS2_PLACEMENT_3D ( 'NONE', #79622, #78874, #12852 ) ;
#32689=LINE ( 'NONE', #31955, #137742 ) ;
#32693=CARTESIAN_POINT ( 'NONE',  ( 66.18398860626901126, 28.73617430169833753, 5.000000000000000000 ) ) ;
#32694=ORIENTED_EDGE ( 'NONE', *, *, #125858, .T. ) ;
#32695=ORIENTED_EDGE ( 'NONE', *, *, #96277, .F. ) ;
#32698=EDGE_CURVE ( 'NONE', #27002, #68801, #111208, .T. ) ;
#32699=VECTOR ( 'NONE', #115219, 1000.000000000000000 ) ;
#32700=DIRECTION ( 'NONE',  ( 1.000000000000000000, 0.000000000000000000, 0.000000000000000000 ) ) ;
#32701=VECTOR ( 'NONE', #107336, 1000.000000000000000 ) ;
#32702=DIRECTION ( 'NONE',  ( 1.000000000000000000, 0.000000000000000000, 0.000000000000000000 ) ) ;
#32703=DIRECTION ( 'NONE',  ( 0.3543493200069162685, -0.000000000000000000, -0.9351131265310288487 ) ) ;
#32704=EDGE_CURVE ( 'NONE', #122378, #42180, #36527, .T. ) ;
#32705=CARTESIAN_POINT ( 'NONE',  ( -54.18398860626899705, 28.73617430169825226, 5.000000000000000000 ) ) ;
#32706=AXIS2_PLACEMENT_3D ( 'NONE', #121141, #9504, #34158 ) ;
#32707=VECTOR ( 'NONE', #32899, 1000.000000000000000 ) ;
#32709=ORIENTED_EDGE ( 'NONE', *, *, #26910, .T. ) ;
#32710=AXIS2_PLACEMENT_3D ( 'NONE', #6297, #138305, #16494 ) ;
#32711=ORIENTED_EDGE ( 'NONE', *, *, #87003, .T. ) ;
#32712=PLANE ( 'NONE',  #134226 ) ;
#32713=ADVANCED_FACE ( 'NONE', ( #11897 ), #35856, .F. ) ;
#32714=AXIS2_PLACEMENT_3D ( 'NONE', #18901, #73309, #108027 ) ;
#32716=VERTEX_POINT ( 'NONE', #124248 ) ;
#32717=ORIENTED_EDGE ( 'NONE', *, *, #125645, .T. ) ;
#32720=AXIS2_PLACEMENT_3D ( 'NONE', #15297, #29070, #71169 ) ;
#32721=LINE ( 'NONE', #9483, #7465 ) ;
#32722=CARTESIAN_POINT ( 'NONE',  ( -26.99999999999980815, -3.033600742197708477, 5.000000000000000000 ) ) ;
#32723=VECTOR ( 'NONE', #90037, 1000.000000000000000 ) ;
#32725=EDGE_LOOP ( 'NONE', ( #37956, #47541, #109246, #92809 ) ) ;
#32726=ADVANCED_FACE ( 'NONE', ( #56891 ), #56186, .F. ) ;
#32727=CARTESIAN_POINT ( 'NONE',  ( 10.49999999999991829, -9.462702396501002866, -9.474982329943541615 ) ) ;
#32728=VERTEX_POINT ( 'NONE', #100369 ) ;
#32729=EDGE_LOOP ( 'NONE', ( #123651, #40812, #102327, #20385 ) ) ;
#32730=ORIENTED_EDGE ( 'NONE', *, *, #132924, .T. ) ;
#32731=ADVANCED_FACE ( 'NONE', ( #58338 ), #79370, .F. ) ;
#32732=ADVANCED_FACE ( 'NONE', ( #101053 ), #33696, .F. ) ;
#32734=DIRECTION ( 'NONE',  ( -0.000000000000000000, 0.3543493200069153248, 0.9351131265310292928 ) ) ;
#32735=ORIENTED_EDGE ( 'NONE', *, *, #87877, .F. ) ;
#32737=CARTESIAN_POINT ( 'NONE',  ( -36.48921356237310221, -27.52281430457080802, 5.000000000000000000 ) ) ;
#32738=VECTOR ( 'NONE', #104453, 1000.000000000000000 ) ;
#32739=ADVANCED_FACE ( 'NONE', ( #24233 ), #134430, .F. ) ;
#32741=FACE_BOUND ( 'NONE', #112179, .T. ) ;
#32742=EDGE_CURVE ( 'NONE', #29861, #80396, #13319, .T. ) ;
#32743=VERTEX_POINT ( 'NONE', #101776 ) ;
#32745=CARTESIAN_POINT ( 'NONE',  ( 31.49999999999977973, 6.431123077392124188, 4.000000000000000000 ) ) ;
#32746=DIRECTION ( 'NONE',  ( -0.7071067811865487940, 0.7071067811865463515, -0.000000000000000000 ) ) ;
#32747=EDGE_CURVE ( 'NONE', #134254, #46293, #34389, .T. ) ;
#32748=ORIENTED_EDGE ( 'NONE', *, *, #58996, .T. ) ;
#32749=LINE ( 'NONE', #110259, #98994 ) ;
#32750=EDGE_LOOP ( 'NONE', ( #47466, #84667, #78307, #31828 ) ) ;
#32752=AXIS2_PLACEMENT_3D ( 'NONE', #118947, #18173, #95044 ) ;
#32753=DIRECTION ( 'NONE',  ( 0.7071067811865486830, -0.7071067811865464625, -0.000000000000000000 ) ) ;
#32754=ORIENTED_EDGE ( 'NONE', *, *, #134173, .T. ) ;
#32756=ORIENTED_EDGE ( 'NONE', *, *, #116842, .T. ) ;
#32757=EDGE_CURVE ( 'NONE', #89225, #142320, #46751, .T. ) ;
#32758=DIRECTION ( 'NONE',  ( 0.6830127018922181881, 0.6830127018922202975, -0.2588190451025214056 ) ) ;
#32759=CARTESIAN_POINT ( 'NONE',  ( 0.000000000000000000, 0.000000000000000000, 5.000000000000000000 ) ) ;
#32760=CARTESIAN_POINT ( 'NONE',  ( 0.1839886062690032631, 28.73617430169787568, 5.000000000000000000 ) ) ;
#32761=ORIENTED_EDGE ( 'NONE', *, *, #66011, .T. ) ;
#32762=LINE ( 'NONE', #120418, #141790 ) ;
#32763=DIRECTION ( 'NONE',  ( 0.7071067811865487940, -0.7071067811865463515, 0.000000000000000000 ) ) ;
#32765=EDGE_CURVE ( 'NONE', #99565, #118931, #122090, .T. ) ;
#32767=VECTOR ( 'NONE', #36470, 999.9999999999998863 ) ;
#32768=PLANE ( 'NONE',  #71062 ) ;
#32770=DIRECTION ( 'NONE',  ( 0.7071067811865487940, 0.7071067811865463515, 0.000000000000000000 ) ) ;
#32771=CARTESIAN_POINT ( 'NONE',  ( -6.707106781186491062, -3.740707523384241728, 5.000000000000000000 ) ) ;
#32772=LINE ( 'NONE', #121171, #67228 ) ;
#32777=AXIS2_PLACEMENT_3D ( 'NONE', #137670, #127484, #125355 ) ;
#32778=VERTEX_POINT ( 'NONE', #111965 ) ;
#32779=VECTOR ( 'NONE', #12345, 1000.000000000000000 ) ;
#32780=DIRECTION ( 'NONE',  ( 0.7071067811865486830, -0.7071067811865464625, -0.000000000000000000 ) ) ;
#32781=LINE ( 'NONE', #21161, #12029 ) ;
#32782=VERTEX_POINT ( 'NONE', #90181 ) ;
#32784=VERTEX_POINT ( 'NONE', #80072 ) ;
#32786=LINE ( 'NONE', #63971, #73398 ) ;
#32787=DIRECTION ( 'NONE',  ( 0.000000000000000000, 1.000000000000000000, 0.000000000000000000 ) ) ;
#32788=VERTEX_POINT ( 'NONE', #113350 ) ;
#32789=VECTOR ( 'NONE', #21972, 999.9999999999998863 ) ;
#32790=CARTESIAN_POINT ( 'NONE',  ( -34.92500000000001137, 5.087954687542278975, -1.493867085284239948 ) ) ;
#32791=ADVANCED_FACE ( 'NONE', ( #102521 ), #101996, .F. ) ;
#32792=CARTESIAN_POINT ( 'NONE',  ( 10.49999999999992539, -1.592773361805362109, -6.492772025301252192 ) ) ;
#32793=ADVANCED_FACE ( 'NONE', ( #58551 ), #23718, .F. ) ;
#32796=VERTEX_POINT ( 'NONE', #80268 ) ;
#32798=VECTOR ( 'NONE', #31490, 1000.000000000000000 ) ;
#32799=DIRECTION ( 'NONE',  ( -0.7071067811865486830, -0.7071067811865464625, 0.000000000000000000 ) ) ;
#32800=DIRECTION ( 'NONE',  ( -0.7071067811865487940, 0.7071067811865463515, -0.000000000000000000 ) ) ;
#32801=DIRECTION ( 'NONE',  ( -0.000000000000000000, 0.3543493200069153248, 0.9351131265310292928 ) ) ;
#32802=VERTEX_POINT ( 'NONE', #46956 ) ;
#32803=DIRECTION ( 'NONE',  ( -0.000000000000000000, 0.000000000000000000, 1.000000000000000000 ) ) ;
#32805=CARTESIAN_POINT ( 'NONE',  ( 24.18398860626899705, 28.73617430169804265, 5.000000000000000000 ) ) ;
#32806=EDGE_CURVE ( 'NONE', #35917, #101850, #111983, .T. ) ;
#32807=LINE ( 'NONE', #24051, #67872 ) ;
#32808=CARTESIAN_POINT ( 'NONE',  ( 48.29974487139158867, -27.71228299555239971, 4.000000000000000000 ) ) ;
#32809=VERTEX_POINT ( 'NONE', #124458 ) ;
#32810=VECTOR ( 'NONE', #85278, 1000.000000000000000 ) ;
#32811=VECTOR ( 'NONE', #130669, 999.9999999999998863 ) ;
#32812=LINE ( 'NONE', #23309, #9432 ) ;
#32814=ORIENTED_EDGE ( 'NONE', *, *, #73298, .F. ) ;
#32816=AXIS2_PLACEMENT_3D ( 'NONE', #58006, #15147, #137686 ) ;
#32817=CARTESIAN_POINT ( 'NONE',  ( 31.49999999999977973, 12.05218569542904206, 5.000000000000000000 ) ) ;
#32819=DIRECTION ( 'NONE',  ( -0.3543493200069162685, -0.000000000000000000, -0.9351131265310288487 ) ) ;
#32821=VERTEX_POINT ( 'NONE', #79586 ) ;
#32822=ORIENTED_EDGE ( 'NONE', *, *, #8071, .F. ) ;
#32823=DIRECTION ( 'NONE',  ( -0.7071067811865486830, -0.7071067811865464625, 0.000000000000000000 ) ) ;
#32824=DIRECTION ( 'NONE',  ( 0.7071067811865486830, -0.7071067811865464625, -0.000000000000000000 ) ) ;
#32825=VECTOR ( 'NONE', #30040, 1000.000000000000114 ) ;
#32826=VERTEX_POINT ( 'NONE', #33897 ) ;
#32827=CARTESIAN_POINT ( 'NONE',  ( 2.999999999999978240, -11.35517001088072142, -1.126524801160101230 ) ) ;
#32828=CARTESIAN_POINT ( 'NONE',  ( -29.99999999999979039, -5.527737879153217015, -7.983877177622302312 ) ) ;
#32829=CARTESIAN_POINT ( 'NONE',  ( 9.328169399223463998, -6.740707523384218192, 4.000000000000000000 ) ) ;
#32832=CARTESIAN_POINT ( 'NONE',  ( 20.99999999999985789, 13.55218569542903140, 5.000000000000000000 ) ) ;
#32833=EDGE_CURVE ( 'NONE', #96928, #84615, #78114, .T. ) ;
#32834=CARTESIAN_POINT ( 'NONE',  ( 36.29974487139159578, -27.71228299555231445, 4.000000000000000000 ) ) ;
#32835=ADVANCED_FACE ( 'NONE', ( #2659 ), #3365, .T. ) ;
#32836=CARTESIAN_POINT ( 'NONE',  ( -17.61782366839360847, 8.969638207445433054, 4.000000000000000000 ) ) ;
#32837=AXIS2_PLACEMENT_3D ( 'NONE', #132866, #47313, #133560 ) ;
#32838=CARTESIAN_POINT ( 'NONE',  ( -34.49999999999976552, 21.43112307739196254, 4.000000000000000000 ) ) ;
#32840=FACE_OUTER_BOUND ( 'NONE', #103371, .T. ) ;
#32841=ORIENTED_EDGE ( 'NONE', *, *, #53790, .F. ) ;
#32842=ORIENTED_EDGE ( 'NONE', *, *, #91289, .T. ) ;
#32843=DIRECTION ( 'NONE',  ( 0.3543493200069162685, -0.000000000000000000, -0.9351131265310288487 ) ) ;
#32844=EDGE_LOOP ( 'NONE', ( #135965, #31890, #123661, #31192 ) ) ;
#32845=VECTOR ( 'NONE', #127418, 1000.000000000000000 ) ;
#32846=ORIENTED_EDGE ( 'NONE', *, *, #130962, .F. ) ;
#32847=AXIS2_PLACEMENT_3D ( 'NONE', #70629, #126379, #94460 ) ;
#32848=LINE ( 'NONE', #42297, #108035 ) ;
#32849=DIRECTION ( 'NONE',  ( 0.7071067811865487940, 0.7071067811865463515, 0.000000000000000000 ) ) ;
#32850=ORIENTED_EDGE ( 'NONE', *, *, #33067, .T. ) ;
#32851=CARTESIAN_POINT ( 'NONE',  ( -28.49999999999979750, 16.46639925780209168, 5.000000000000000000 ) ) ;
#32852=CARTESIAN_POINT ( 'NONE',  ( 33.70710678118631165, 2.259292476615694323, 5.000000000000000000 ) ) ;
#32854=DIRECTION ( 'NONE',  ( 0.3543493200069162685, -0.000000000000000000, -0.9351131265310288487 ) ) ;
#32855=PLANE ( 'NONE',  #122868 ) ;
#32857=EDGE_CURVE ( 'NONE', #93902, #3598, #111432, .T. ) ;
#32858=EDGE_LOOP ( 'NONE', ( #73386, #18242, #123655, #29469, #123225 ) ) ;
#32859=DIRECTION ( 'NONE',  ( -0.7071067811865486830, -0.7071067811865464625, 0.000000000000000000 ) ) ;
#32860=DIRECTION ( 'NONE',  ( -0.000000000000000000, -0.3543493200069152693, 0.9351131265310292928 ) ) ;
#32861=DIRECTION ( 'NONE',  ( -0.000000000000000000, 0.000000000000000000, 1.000000000000000000 ) ) ;
#32862=DIRECTION ( 'NONE',  ( 0.7071067811865487940, 0.7071067811865463515, -0.000000000000000000 ) ) ;
#32866=ADVANCED_FACE ( 'NONE', ( #67232 ), #45507, .F. ) ;
#32868=EDGE_CURVE ( 'NONE', #115465, #49398, #36728, .T. ) ;
#32869=PLANE ( 'NONE',  #93016 ) ;
#32872=EDGE_LOOP ( 'NONE', ( #58309, #94468, #4134, #49446 ) ) ;
#32874=ADVANCED_FACE ( 'NONE', ( #12113 ), #78833, .F. ) ;
#32875=DIRECTION ( 'NONE',  ( 0.7071067811865487940, -0.7071067811865463515, 0.000000000000000000 ) ) ;
#32876=CARTESIAN_POINT ( 'NONE',  ( -34.49999999999975131, 16.08746187583907528, 4.000000000000000000 ) ) ;
#32877=VERTEX_POINT ( 'NONE', #123043 ) ;
#32878=CIRCLE ( 'NONE', #30688, 5.968999999999998529 ) ;
#32879=VECTOR ( 'NONE', #82021, 1000.000000000000227 ) ;
#32881=LINE ( 'NONE', #119826, #46989 ) ;
#32883=EDGE_CURVE ( 'NONE', #119795, #22356, #47659, .T. ) ;
#32884=VECTOR ( 'NONE', #23249, 1000.000000000000000 ) ;
#32886=VERTEX_POINT ( 'NONE', #69384 ) ;
#32889=ORIENTED_EDGE ( 'NONE', *, *, #99630, .T. ) ;
#32890=VECTOR ( 'NONE', #140353, 999.9999999999998863 ) ;
#32891=VECTOR ( 'NONE', #120711, 1000.000000000000000 ) ;
#32892=VECTOR ( 'NONE', #81764, 1000.000000000000000 ) ;
#32893=DIRECTION ( 'NONE',  ( -0.6830127018922181881, 0.6830127018922202975, -0.2588190451025214056 ) ) ;
#32894=EDGE_CURVE ( 'NONE', #106547, #77537, #514, .T. ) ;
#32895=LINE ( 'NONE', #21971, #31455 ) ;
#32896=DIRECTION ( 'NONE',  ( 0.7071067811865486830, -0.7071067811865464625, -0.000000000000000000 ) ) ;
#32897=CARTESIAN_POINT ( 'NONE',  ( -20.99451991528748707, 28.92564299267952777, 4.000000000000000000 ) ) ;
#32898=ORIENTED_EDGE ( 'NONE', *, *, #93750, .F. ) ;
#32899=DIRECTION ( 'NONE',  ( -0.7071067811865486830, -0.7071067811865464625, -0.000000000000000000 ) ) ;
#32900=CARTESIAN_POINT ( 'NONE',  ( 5.994519915287488843, 28.92564299267942118, 4.000000000000000000 ) ) ;
#32901=ORIENTED_EDGE ( 'NONE', *, *, #7903, .T. ) ;
#32903=DIRECTION ( 'NONE',  ( -0.7071067811865487940, 0.7071067811865463515, -0.000000000000000000 ) ) ;
#32906=EDGE_CURVE ( 'NONE', #70409, #39875, #90400, .T. ) ;
#32907=CARTESIAN_POINT ( 'NONE',  ( 16.49999999999989342, 10.08746187583914278, 4.000000000000000000 ) ) ;
#32909=CARTESIAN_POINT ( 'NONE',  ( 30.70710678118632941, 2.259292476615694323, 5.000000000000000000 ) ) ;
#32911=DIRECTION ( 'NONE',  ( 0.7071067811865487940, 0.7071067811865463515, 0.000000000000000000 ) ) ;
#32912=EDGE_CURVE ( 'NONE', #42695, #92475, #91145, .T. ) ;
#32913=LINE ( 'NONE', #45226, #96385 ) ;
#32914=ORIENTED_EDGE ( 'NONE', *, *, #7175, .F. ) ;
#32915=VERTEX_POINT ( 'NONE', #13527 ) ;
#32916=PLANE ( 'NONE',  #2892 ) ;
#32917=VERTEX_POINT ( 'NONE', #113569 ) ;
#32918=VECTOR ( 'NONE', #116532, 1000.000000000000000 ) ;
#32919=EDGE_CURVE ( 'NONE', #53913, #98731, #102719, .T. ) ;
#32920=ORIENTED_EDGE ( 'NONE', *, *, #30820, .T. ) ;
#32921=VECTOR ( 'NONE', #121484, 1000.000000000000000 ) ;
#32922=CARTESIAN_POINT ( 'NONE',  ( 11.99999999999992184, 13.93112307739204425, 4.000000000000000000 ) ) ;
#32924=ADVANCED_FACE ( 'NONE', ( #51199 ), #128056, .F. ) ;
#32925=AXIS2_PLACEMENT_3D ( 'NONE', #37596, #69523, #93387 ) ;
#32926=CARTESIAN_POINT ( 'NONE',  ( -27.29974487139158512, -27.71228299555225405, 4.000000000000000000 ) ) ;
#32928=AXIS2_PLACEMENT_3D ( 'NONE', #33585, #121266, #22638 ) ;
#32929=EDGE_CURVE ( 'NONE', #114916, #3959, #28009, .T. ) ;
#32930=LINE ( 'NONE', #111892, #102127 ) ;
#32931=FACE_BOUND ( 'NONE', #58786, .T. ) ;
#32932=CARTESIAN_POINT ( 'NONE',  ( -16.00193056682086379, -22.22500000000000142, 4.500000000000000888 ) ) ;
#32934=DIRECTION ( 'NONE',  ( 0.7071067811865486830, -0.7071067811865464625, -0.000000000000000000 ) ) ;
#32936=ORIENTED_EDGE ( 'NONE', *, *, #89146, .F. ) ;
#32938=CARTESIAN_POINT ( 'NONE',  ( 15.29974487139158867, -27.71228299555216879, 4.000000000000000000 ) ) ;
#32940=ORIENTED_EDGE ( 'NONE', *, *, #89196, .T. ) ;
#32941=ORIENTED_EDGE ( 'NONE', *, *, #75131, .F. ) ;
#32944=DIRECTION ( 'NONE',  ( -0.7071067811865486830, 0.7071067811865463515, 0.000000000000000000 ) ) ;
#32945=EDGE_CURVE ( 'NONE', #55371, #130377, #27699, .T. ) ;
#32946=DIRECTION ( 'NONE',  ( -0.7071067811865486830, -0.7071067811865464625, -0.000000000000000000 ) ) ;
#32947=VECTOR ( 'NONE', #5569, 1000.000000000000227 ) ;
#32948=ORIENTED_EDGE ( 'NONE', *, *, #124506, .T. ) ;
#32949=DIRECTION ( 'NONE',  ( -0.7071067811865486830, -0.7071067811865464625, 0.000000000000000000 ) ) ;
#32951=EDGE_CURVE ( 'NONE', #59015, #76484, #27271, .T. ) ;
#32952=CARTESIAN_POINT ( 'NONE',  ( -26.33153258840125588, -18.74070752338408496, 20.73178291233834969 ) ) ;
#32954=DIRECTION ( 'NONE',  ( 0.3543493200069162685, -0.000000000000000000, -0.9351131265310288487 ) ) ;
#32955=CARTESIAN_POINT ( 'NONE',  ( -21.29974487139158512, -27.71228299555221142, 4.000000000000000000 ) ) ;
#32956=DIRECTION ( 'NONE',  ( 0.6830127018922181881, 0.6830127018922202975, -0.2588190451025214056 ) ) ;
#32957=LINE ( 'NONE', #10435, #70154 ) ;
#32959=ORIENTED_EDGE ( 'NONE', *, *, #58131, .F. ) ;
#32961=FACE_OUTER_BOUND ( 'NONE', #3191, .T. ) ;
#32962=ORIENTED_EDGE ( 'NONE', *, *, #77346, .T. ) ;
#32963=CARTESIAN_POINT ( 'NONE',  ( -18.18398860626898994, 28.73617430169800002, 5.000000000000000000 ) ) ;
#32965=ORIENTED_EDGE ( 'NONE', *, *, #109148, .T. ) ;
#32966=VERTEX_POINT ( 'NONE', #137491 ) ;
#32967=ADVANCED_FACE ( 'NONE', ( #136751 ), #128740, .F. ) ;
#32969=VECTOR ( 'NONE', #77600, 1000.000000000000000 ) ;
#32970=ORIENTED_EDGE ( 'NONE', *, *, #75996, .F. ) ;
#32971=CARTESIAN_POINT ( 'NONE',  ( 34.42499999999998295, 22.22500000000000142, 5.000000000000000000 ) ) ;
#32973=LINE ( 'NONE', #142430, #100226 ) ;
#32977=CARTESIAN_POINT ( 'NONE',  ( 32.99999999999977973, -7.447814304570745669, 5.000000000000000000 ) ) ;
#32979=CARTESIAN_POINT ( 'NONE',  ( -51.48921356237309510, -27.52281430457091460, 5.000000000000000000 ) ) ;
#32980=CARTESIAN_POINT ( 'NONE',  ( -32.99999999999976552, 2.966399257802230682, 5.000000000000000000 ) ) ;
#32981=VECTOR ( 'NONE', #74551, 1000.000000000000000 ) ;
#32982=VECTOR ( 'NONE', #51878, 1000.000000000000000 ) ;
#32983=CARTESIAN_POINT ( 'NONE',  ( -2.700255128608413990, -27.71228299555204089, 4.000000000000000000 ) ) ;
#32985=AXIS2_PLACEMENT_3D ( 'NONE', #108615, #41989, #10737 ) ;
#32988=LINE ( 'NONE', #14763, #44587 ) ;
#32989=DIRECTION ( 'NONE',  ( 0.7071067811865487940, 0.7071067811865463515, 0.000000000000000000 ) ) ;
#32990=AXIS2_PLACEMENT_3D ( 'NONE', #50039, #94231, #127591 ) ;
#32991=VERTEX_POINT ( 'NONE', #114966 ) ;
#32992=EDGE_CURVE ( 'NONE', #22931, #27577, #83851, .T. ) ;
#32993=FACE_OUTER_BOUND ( 'NONE', #103642, .T. ) ;
#32994=ORIENTED_EDGE ( 'NONE', *, *, #17095, .F. ) ;
#32995=ORIENTED_EDGE ( 'NONE', *, *, #78088, .F. ) ;
#32996=DIRECTION ( 'NONE',  ( 0.7071067811865486830, -0.7071067811865464625, -0.000000000000000000 ) ) ;
#32997=LINE ( 'NONE', #28858, #81103 ) ;
#32998=VECTOR ( 'NONE', #87236, 1000.000000000000000 ) ;
#32999=VECTOR ( 'NONE', #14085, 1000.000000000000000 ) ;
#33001=CARTESIAN_POINT ( 'NONE',  ( -1.499999999999990896, -12.66682484999666514, -0.6294897503863975396 ) ) ;
#33002=CARTESIAN_POINT ( 'NONE',  ( -32.99999999999976552, -19.44781430457063465, 5.000000000000000000 ) ) ;
#33003=PLANE ( 'NONE',  #102419 ) ;
#33004=CARTESIAN_POINT ( 'NONE',  ( 45.29974487139158867, -27.71228299555237840, 4.000000000000000000 ) ) ;
#33005=CARTESIAN_POINT ( 'NONE',  ( -23.99451991528749062, 28.92564299267954908, 4.000000000000000000 ) ) ;
#33007=ORIENTED_EDGE ( 'NONE', *, *, #28259, .F. ) ;
#33009=ORIENTED_EDGE ( 'NONE', *, *, #12518, .F. ) ;
#33012=CARTESIAN_POINT ( 'NONE',  ( -2.483345613589531542, 22.22500000000000142, 4.500000000000000888 ) ) ;
#33014=FACE_OUTER_BOUND ( 'NONE', #107807, .T. ) ;
#33015=CARTESIAN_POINT ( 'NONE',  ( -17.20710678118642178, -5.240707523384227073, 5.000000000000000000 ) ) ;
#33016=DIRECTION ( 'NONE',  ( -0.7071067811865487940, 0.7071067811865463515, 0.000000000000000000 ) ) ;
#33017=VERTEX_POINT ( 'NONE', #38183 ) ;
#33018=FACE_OUTER_BOUND ( 'NONE', #20180, .T. ) ;
#33019=LINE ( 'NONE', #43868, #139161 ) ;
#33021=DIRECTION ( 'NONE',  ( 0.7071067811865486830, -0.7071067811865464625, -0.000000000000000000 ) ) ;
#33023=CARTESIAN_POINT ( 'NONE',  ( 26.99451991528749417, 28.92564299267956685, 4.000000000000000000 ) ) ;
#33025=VECTOR ( 'NONE', #72196, 1000.000000000000227 ) ;
#33026=LINE ( 'NONE', #101086, #115849 ) ;
#33027=CARTESIAN_POINT ( 'NONE',  ( 50.99451991528749062, 28.92564299267973738, 4.000000000000000000 ) ) ;
#33029=LINE ( 'NONE', #122123, #58042 ) ;
#33031=EDGE_LOOP ( 'NONE', ( #74336, #62964, #76995, #107618, #86423 ) ) ;
#33032=CARTESIAN_POINT ( 'NONE',  ( -23.20710678118638270, 9.759292476615620160, 5.000000000000000000 ) ) ;
#33033=EDGE_CURVE ( 'NONE', #56766, #2192, #5510, .T. ) ;
#33034=ORIENTED_EDGE ( 'NONE', *, *, #126966, .F. ) ;
#33036=DIRECTION ( 'NONE',  ( -0.7071067811865487940, 0.7071067811865463515, -0.000000000000000000 ) ) ;
#33037=DIRECTION ( 'NONE',  ( -0.000000000000000000, -0.3543493200069152693, 0.9351131265310292928 ) ) ;
#33040=DIRECTION ( 'NONE',  ( -0.7071067811865487940, 0.7071067811865463515, -0.000000000000000000 ) ) ;
#33041=CARTESIAN_POINT ( 'NONE',  ( -8.816011393731004731, 28.73617430169781173, 5.000000000000000000 ) ) ;
#33042=CARTESIAN_POINT ( 'NONE',  ( -50.99451991528749062, 28.92564299267973738, 4.000000000000000000 ) ) ;
#33043=CARTESIAN_POINT ( 'NONE',  ( 0.005480084712502889671, 28.92564299267938210, 4.000000000000000000 ) ) ;
#33044=EDGE_CURVE ( 'NONE', #2192, #36781, #49789, .T. ) ;
#33045=EDGE_CURVE ( 'NONE', #38188, #121396, #82399, .T. ) ;
#33046=ORIENTED_EDGE ( 'NONE', *, *, #13865, .T. ) ;
#33047=ORIENTED_EDGE ( 'NONE', *, *, #142211, .F. ) ;
#33048=CARTESIAN_POINT ( 'NONE',  ( 1.499999999999990896, -7.533600742197664069, 5.000000000000000000 ) ) ;
#33051=CARTESIAN_POINT ( 'NONE',  ( -19.05000000000000071, 3.174999999999997158, 4.000000000000000000 ) ) ;
#33053=EDGE_CURVE ( 'NONE', #122674, #122361, #50480, .T. ) ;
#33055=ADVANCED_FACE ( 'NONE', ( #71523 ), #38883, .F. ) ;
#33056=CARTESIAN_POINT ( 'NONE',  ( -32.91685193227049666, 21.75929247661549581, 7.311836541447975790 ) ) ;
#33057=DIRECTION ( 'NONE',  ( -0.3543493200069163240, -0.000000000000000000, 0.9351131265310288487 ) ) ;
#33059=ADVANCED_FACE ( 'NONE', ( #127307 ), #72979, .F. ) ;
#33061=DIRECTION ( 'NONE',  ( -0.6830127018922181881, 0.6830127018922202975, -0.2588190451025214056 ) ) ;
#33063=LINE ( 'NONE', #32317, #110906 ) ;
#33064=DIRECTION ( 'NONE',  ( 0.6830127018922180770, -0.6830127018922204085, -0.2588190451025213501 ) ) ;
#33065=VECTOR ( 'NONE', #101156, 1000.000000000000000 ) ;
#33067=EDGE_CURVE ( 'NONE', #5308, #139710, #117135, .T. ) ;
#33068=ORIENTED_EDGE ( 'NONE', *, *, #32077, .T. ) ;
#33070=ADVANCED_FACE ( 'NONE', ( #9051 ), #76531, .F. ) ;
#33071=ORIENTED_EDGE ( 'NONE', *, *, #2782, .T. ) ;
#33072=DIRECTION ( 'NONE',  ( -0.7071067811865486830, -0.7071067811865464625, 0.000000000000000000 ) ) ;
#33074=PLANE ( 'NONE',  #82506 ) ;
#33075=ORIENTED_EDGE ( 'NONE', *, *, #30382, .F. ) ;
#33076=FACE_OUTER_BOUND ( 'NONE', #34027, .T. ) ;
#33077=PLANE ( 'NONE',  #91573 ) ;
#33079=DIRECTION ( 'NONE',  ( 0.3543493200069162685, -0.000000000000000000, -0.9351131265310288487 ) ) ;
#33080=CARTESIAN_POINT ( 'NONE',  ( -2.395137668124769359, 21.75929247661549937, 21.32995629748187483 ) ) ;
#33081=CARTESIAN_POINT ( 'NONE',  ( 8.510786437626906675, -27.52281430457049183, 5.000000000000000000 ) ) ;
#33082=CARTESIAN_POINT ( 'NONE',  ( -15.97910837819034668, 22.22500000000000142, -2.179306570123547893 ) ) ;
#33083=ORIENTED_EDGE ( 'NONE', *, *, #45574, .F. ) ;
#33084=DIRECTION ( 'NONE',  ( 0.3543493200069162685, -0.000000000000000000, -0.9351131265310288487 ) ) ;
#33085=VECTOR ( 'NONE', #135567, 1000.000000000000000 ) ;
#33086=EDGE_CURVE ( 'NONE', #92724, #103666, #21419, .T. ) ;
#33087=CARTESIAN_POINT ( 'NONE',  ( 34.92499999999998295, -21.72500000000000142, 5.000000000000000000 ) ) ;
#33088=ORIENTED_EDGE ( 'NONE', *, *, #123194, .F. ) ;
#33089=ORIENTED_EDGE ( 'NONE', *, *, #5648, .F. ) ;
#33091=ORIENTED_EDGE ( 'NONE', *, *, #77083, .T. ) ;
#33092=LINE ( 'NONE', #392, #33718 ) ;
#33093=DIRECTION ( 'NONE',  ( -0.000000000000000000, -0.3543493200069152693, 0.9351131265310292928 ) ) ;
#33095=DIRECTION ( 'NONE',  ( -0.000000000000000000, 0.3543493200069153248, 0.9351131265310292928 ) ) ;
#33096=ORIENTED_EDGE ( 'NONE', *, *, #63013, .F. ) ;
#33097=EDGE_LOOP ( 'NONE', ( #119140, #76329, #86983, #78993 ) ) ;
#33098=VECTOR ( 'NONE', #65453, 1000.000000000000000 ) ;
#33099=VECTOR ( 'NONE', #108998, 999.9999999999998863 ) ;
#33100=CARTESIAN_POINT ( 'NONE',  ( 9.328169399223469327, 14.25929247661557575, 4.000000000000000000 ) ) ;
#33101=LINE ( 'NONE', #41795, #51396 ) ;
#33102=AXIS2_PLACEMENT_3D ( 'NONE', #8662, #129774, #74714 ) ;
#33104=EDGE_CURVE ( 'NONE', #125114, #76630, #119973, .T. ) ;
#33105=ORIENTED_EDGE ( 'NONE', *, *, #3227, .F. ) ;
#33106=CARTESIAN_POINT ( 'NONE',  ( 29.48831394071549994, 6.759292476615649470, 16.35960578974462720 ) ) ;
#33107=EDGE_CURVE ( 'NONE', #69740, #13073, #118573, .T. ) ;
#33108=VECTOR ( 'NONE', #90162, 1000.000000000000000 ) ;
#33109=CARTESIAN_POINT ( 'NONE',  ( -34.92500000000001137, -6.281509562795707602, 4.759050581649337808 ) ) ;
#33110=CARTESIAN_POINT ( 'NONE',  ( -7.499999999999944045, -6.839392718269134974, -8.480912228396066510 ) ) ;
#33111=AXIS2_PLACEMENT_3D ( 'NONE', #12847, #57126, #124487 ) ;
#33113=EDGE_CURVE ( 'NONE', #79922, #107272, #64215, .T. ) ;
#33114=VERTEX_POINT ( 'NONE', #74388 ) ;
#33115=LINE ( 'NONE', #87460, #75502 ) ;
#33118=CARTESIAN_POINT ( 'NONE',  ( -5.999999999999956479, -22.06887692260758982, 4.000000000000000000 ) ) ;
#33119=LINE ( 'NONE', #65011, #29540 ) ;
#33120=DIRECTION ( 'NONE',  ( 0.6830127018922181881, 0.6830127018922202975, -0.2588190451025214056 ) ) ;
#33121=ORIENTED_EDGE ( 'NONE', *, *, #73479, .T. ) ;
#33122=VECTOR ( 'NONE', #21400, 999.9999999999998863 ) ;
#33123=ORIENTED_EDGE ( 'NONE', *, *, #131921, .F. ) ;
#33125=ORIENTED_EDGE ( 'NONE', *, *, #121610, .T. ) ;
#33126=EDGE_CURVE ( 'NONE', #56496, #130555, #43891, .T. ) ;
#33127=ORIENTED_EDGE ( 'NONE', *, *, #88249, .T. ) ;
#33128=CARTESIAN_POINT ( 'NONE',  ( 20.99999999999985789, -3.412538124160721331, 4.000000000000000000 ) ) ;
#33129=AXIS2_PLACEMENT_3D ( 'NONE', #71639, #138314, #118691 ) ;
#33130=LINE ( 'NONE', #131690, #22278 ) ;
#33133=LINE ( 'NONE', #77348, #119964 ) ;
#33134=CARTESIAN_POINT ( 'NONE',  ( 15.18398860626900237, 28.73617430169797871, 5.000000000000000000 ) ) ;
#33135=EDGE_CURVE ( 'NONE', #48771, #117579, #106980, .T. ) ;
#33136=PLANE ( 'NONE',  #87088 ) ;
#33138=DIRECTION ( 'NONE',  ( -0.7071067811865487940, 0.7071067811865463515, -0.000000000000000000 ) ) ;
#33140=LINE ( 'NONE', #136676, #127127 ) ;
#33143=ORIENTED_EDGE ( 'NONE', *, *, #121401, .T. ) ;
#33144=DIRECTION ( 'NONE',  ( -1.000000000000000000, 0.000000000000000000, 0.000000000000000000 ) ) ;
#33146=ORIENTED_EDGE ( 'NONE', *, *, #40854, .T. ) ;
#33148=ORIENTED_EDGE ( 'NONE', *, *, #112245, .F. ) ;
#33151=EDGE_LOOP ( 'NONE', ( #45892, #39255, #71292, #131107 ) ) ;
#33152=VECTOR ( 'NONE', #25301, 1000.000000000000227 ) ;
#33153=CARTESIAN_POINT ( 'NONE',  ( 60.29974487139158867, -27.71228299555248142, 4.000000000000000000 ) ) ;
#33157=LINE ( 'NONE', #52706, #37927 ) ;
#33158=VECTOR ( 'NONE', #92237, 1000.000000000000000 ) ;
#33159=EDGE_LOOP ( 'NONE', ( #110584, #49942, #5798, #124110 ) ) ;
#33161=VECTOR ( 'NONE', #82951, 1000.000000000000000 ) ;
#33162=CARTESIAN_POINT ( 'NONE',  ( 27.18398860626900060, 28.73617430169806042, 5.000000000000000000 ) ) ;
#33163=EDGE_CURVE ( 'NONE', #34776, #137982, #130191, .T. ) ;
#33164=LINE ( 'NONE', #77374, #88441 ) ;
#33166=VERTEX_POINT ( 'NONE', #98269 ) ;
#33167=EDGE_CURVE ( 'NONE', #139146, #42711, #85224, .T. ) ;
#33169=ORIENTED_EDGE ( 'NONE', *, *, #103146, .F. ) ;
#33170=EDGE_LOOP ( 'NONE', ( #136809, #137754, #84358, #141153 ) ) ;
#33171=ORIENTED_EDGE ( 'NONE', *, *, #72625, .T. ) ;
#33173=VECTOR ( 'NONE', #26923, 1000.000000000000000 ) ;
#33174=DIRECTION ( 'NONE',  ( 0.6830127018922180770, -0.6830127018922204085, -0.2588190451025213501 ) ) ;
#33175=CARTESIAN_POINT ( 'NONE',  ( 20.48334561358940675, 22.22500000000000142, 4.500000000000000888 ) ) ;
#33176=ADVANCED_FACE ( 'NONE', ( #43181 ), #53314, .F. ) ;
#33177=ORIENTED_EDGE ( 'NONE', *, *, #12723, .T. ) ;
#33178=DIRECTION ( 'NONE',  ( -0.000000000000000000, 0.000000000000000000, 1.000000000000000000 ) ) ;
#33179=VECTOR ( 'NONE', #41219, 1000.000000000000227 ) ;
#33182=FACE_OUTER_BOUND ( 'NONE', #10565, .T. ) ;
#33184=DIRECTION ( 'NONE',  ( 0.6830127018922180770, -0.6830127018922204085, -0.2588190451025213501 ) ) ;
#33185=VERTEX_POINT ( 'NONE', #141785 ) ;
#33187=VERTEX_POINT ( 'NONE', #108374 ) ;
#33188=CARTESIAN_POINT ( 'NONE',  ( 15.00548008471250228, 28.92564299267927552, 4.000000000000000000 ) ) ;
#33189=CARTESIAN_POINT ( 'NONE',  ( 34.49999999999975842, -13.53574439159937093, 4.994342998332162331 ) ) ;
#33191=VECTOR ( 'NONE', #28351, 999.9999999999998863 ) ;
#33192=DIRECTION ( 'NONE',  ( -0.7071067811865486830, 0.7071067811865464625, 0.000000000000000000 ) ) ;
#33193=LINE ( 'NONE', #87533, #43630 ) ;
#33194=AXIS2_PLACEMENT_3D ( 'NONE', #18828, #76086, #64490 ) ;
#33195=LINE ( 'NONE', #9203, #41479 ) ;
#33196=CARTESIAN_POINT ( 'NONE',  ( -15.00548008471250228, 28.92564299267927552, 4.000000000000000000 ) ) ;
#33197=LINE ( 'NONE', #66511, #104217 ) ;
#33198=DIRECTION ( 'NONE',  ( -0.7071067811865486830, -0.7071067811865464625, 0.000000000000000000 ) ) ;
#33199=ORIENTED_EDGE ( 'NONE', *, *, #84145, .F. ) ;
#33200=FACE_OUTER_BOUND ( 'NONE', #62329, .T. ) ;
#33201=EDGE_CURVE ( 'NONE', #66673, #76695, #65684, .T. ) ;
#33202=VECTOR ( 'NONE', #128457, 1000.000000000000000 ) ;
#33204=EDGE_LOOP ( 'NONE', ( #109688, #112558, #123431, #117064 ) ) ;
#33205=LINE ( 'NONE', #8501, #96203 ) ;
#33209=CARTESIAN_POINT ( 'NONE',  ( 0.000000000000000000, 0.000000000000000000, 5.000000000000000000 ) ) ;
#33210=ORIENTED_EDGE ( 'NONE', *, *, #56265, .F. ) ;
#33211=CARTESIAN_POINT ( 'NONE',  ( 24.48921356237309510, -27.52281430457072631, 5.000000000000000000 ) ) ;
#33212=ADVANCED_FACE ( 'NONE', ( #18520 ), #30883, .F. ) ;
#33213=VERTEX_POINT ( 'NONE', #41741 ) ;
#33214=DIRECTION ( 'NONE',  ( 0.7071067811865487940, -0.7071067811865463515, 0.000000000000000000 ) ) ;
#33216=LINE ( 'NONE', #91149, #106831 ) ;
#33217=VERTEX_POINT ( 'NONE', #119280 ) ;
#33220=EDGE_CURVE ( 'NONE', #49530, #128364, #107693, .T. ) ;
#33222=VECTOR ( 'NONE', #58905, 999.9999999999998863 ) ;
#33223=CARTESIAN_POINT ( 'NONE',  ( 6.792893218813409462, 9.759292476615618384, 5.000000000000000000 ) ) ;
#33225=CARTESIAN_POINT ( 'NONE',  ( 9.183988606268997046, 28.73617430169793607, 5.000000000000000000 ) ) ;
#33226=LINE ( 'NONE', #99116, #82057 ) ;
#33227=EDGE_CURVE ( 'NONE', #86031, #41563, #68515, .T. ) ;
#33228=DIRECTION ( 'NONE',  ( -0.7071067811865486830, 0.7071067811865464625, 0.000000000000000000 ) ) ;
#33233=ADVANCED_FACE ( 'NONE', ( #46792 ), #23550, .T. ) ;
#33234=ORIENTED_EDGE ( 'NONE', *, *, #71873, .F. ) ;
#33235=VECTOR ( 'NONE', #6864, 1000.000000000000227 ) ;
#33236=ORIENTED_EDGE ( 'NONE', *, *, #26211, .F. ) ;
#33237=CARTESIAN_POINT ( 'NONE',  ( -0.6567100016621301162, 3.759292476615681888, 13.27625715073265589 ) ) ;
#33239=VECTOR ( 'NONE', #49574, 1000.000000000000227 ) ;
#33240=ADVANCED_FACE ( 'NONE', ( #58381 ), #113397, .F. ) ;
#33242=DIRECTION ( 'NONE',  ( -0.7071067811865486830, -0.7071067811865464625, 0.000000000000000000 ) ) ;
#33243=DIRECTION ( 'NONE',  ( -0.000000000000000000, 0.000000000000000000, 1.000000000000000000 ) ) ;
#33245=ORIENTED_EDGE ( 'NONE', *, *, #39293, .T. ) ;
#33247=VECTOR ( 'NONE', #12625, 999.9999999999998863 ) ;
#33248=EDGE_CURVE ( 'NONE', #23925, #43233, #110532, .T. ) ;
#33249=CARTESIAN_POINT ( 'NONE',  ( -10.49999999999992184, 7.466399257802187606, 5.000000000000000000 ) ) ;
#33250=EDGE_CURVE ( 'NONE', #120007, #115599, #46046, .T. ) ;
#33252=CARTESIAN_POINT ( 'NONE',  ( 5.999999999999966249, 19.55218569542897100, 5.000000000000000000 ) ) ;
#33253=DIRECTION ( 'NONE',  ( -0.000000000000000000, -0.3543493200069152693, 0.9351131265310292928 ) ) ;
#33254=ORIENTED_EDGE ( 'NONE', *, *, #89794, .T. ) ;
#33256=LINE ( 'NONE', #66562, #84736 ) ;
#33257=LINE ( 'NONE', #52792, #42372 ) ;
#33259=EDGE_CURVE ( 'NONE', #111034, #22009, #67817, .T. ) ;
#33261=AXIS2_PLACEMENT_3D ( 'NONE', #22880, #35261, #2571 ) ;
#33262=EDGE_LOOP ( 'NONE', ( #125849, #35592, #130870, #125908 ) ) ;
#33263=ORIENTED_EDGE ( 'NONE', *, *, #69953, .F. ) ;
#33264=EDGE_LOOP ( 'NONE', ( #21969, #119526, #126602, #45137 ) ) ;
#33266=AXIS2_PLACEMENT_3D ( 'NONE', #93931, #105508, #137458 ) ;
#33267=( BOUNDED_CURVE ( )  B_SPLINE_CURVE ( 3, ( #7461, #106052, #72076, #72803 ),
 .UNSPECIFIED., .F., .T. ) 
 B_SPLINE_CURVE_WITH_KNOTS ( ( 4, 4 ),
 ( 5.920967161967927161, 7.341195215986605405 ),
 .UNSPECIFIED. ) 
 CURVE ( )  GEOMETRIC_REPRESENTATION_ITEM ( )  RATIONAL_B_SPLINE_CURVE ( ( 1.000000000000000000, 0.8388583629366683780, 0.8388583629366683780, 1.000000000000000000 ) ) 
 REPRESENTATION_ITEM ( '' )  );
#33268=ORIENTED_EDGE ( 'NONE', *, *, #73052, .F. ) ;
#33269=CARTESIAN_POINT ( 'NONE',  ( 14.95136400821897205, -1.164498636767094197, 4.123993368336929422 ) ) ;
#33270=VECTOR ( 'NONE', #87585, 1000.000000000000000 ) ;
#33273=DIRECTION ( 'NONE',  ( -0.7071067811865486830, 0.7071067811865464625, 0.000000000000000000 ) ) ;
#33274=CARTESIAN_POINT ( 'NONE',  ( -16.82334089840016844, 5.259292476615659240, 15.86257073897101577 ) ) ;
#33276=ORIENTED_EDGE ( 'NONE', *, *, #19685, .F. ) ;
#33278=EDGE_CURVE ( 'NONE', #18830, #26483, #100412, .T. ) ;
#33280=CARTESIAN_POINT ( 'NONE',  ( -34.75611968250420603, 11.81293425470724578, 4.955485411084898040 ) ) ;
#33281=VERTEX_POINT ( 'NONE', #44642 ) ;
#33282=ORIENTED_EDGE ( 'NONE', *, *, #15419, .F. ) ;
#33283=VERTEX_POINT ( 'NONE', #3208 ) ;
#33284=DIRECTION ( 'NONE',  ( -0.000000000000000000, 0.000000000000000000, 1.000000000000000000 ) ) ;
#33285=LINE ( 'NONE', #65905, #100948 ) ;
#33287=VECTOR ( 'NONE', #137363, 1000.000000000000000 ) ;
#33288=FACE_OUTER_BOUND ( 'NONE', #44666, .T. ) ;
#33289=DIRECTION ( 'NONE',  ( 0.7071067811865487940, 0.7071067811865463515, 0.000000000000000000 ) ) ;
#33290=ADVANCED_FACE ( 'NONE', ( #45343 ), #35172, .T. ) ;
#33291=CARTESIAN_POINT ( 'NONE',  ( -48.48921356237309510, -27.52281430457089328, 5.000000000000000000 ) ) ;
#33293=SURFACE_SIDE_STYLE ('',( #20922 ) ) ;
#33294=AXIS2_PLACEMENT_3D ( 'NONE', #36840, #125290, #133328 ) ;
#33296=ORIENTED_EDGE ( 'NONE', *, *, #59393, .F. ) ;
#33297=DIRECTION ( 'NONE',  ( -0.7071067811865487940, 0.7071067811865463515, 0.000000000000000000 ) ) ;
#33298=EDGE_CURVE ( 'NONE', #90674, #24049, #88830, .T. ) ;
#33300=EDGE_LOOP ( 'NONE', ( #119781, #71877, #16374, #79122 ) ) ;
#33301=AXIS2_PLACEMENT_3D ( 'NONE', #35474, #46352, #68114 ) ;
#33302=CARTESIAN_POINT ( 'NONE',  ( -54.48921356237310221, -27.52281430457093236, 5.000000000000000000 ) ) ;
#33303=VERTEX_POINT ( 'NONE', #135203 ) ;
#33307=CARTESIAN_POINT ( 'NONE',  ( 34.49999999999975842, -19.53574439159931231, 4.994342998332164107 ) ) ;
#33308=CARTESIAN_POINT ( 'NONE',  ( 34.92499999999998295, 22.22500000000000142, 4.000000000000000000 ) ) ;
#33309=CARTESIAN_POINT ( 'NONE',  ( 5.292893218813423672, 2.259292476615697876, 5.000000000000000000 ) ) ;
#33310=VERTEX_POINT ( 'NONE', #22105 ) ;
#33311=DIRECTION ( 'NONE',  ( 0.3543493200069162685, -0.000000000000000000, -0.9351131265310288487 ) ) ;
#33312=ORIENTED_EDGE ( 'NONE', *, *, #136141, .T. ) ;
#33314=ADVANCED_FACE ( 'NONE', ( #99668 ), #133059, .T. ) ;
#33315=VERTEX_POINT ( 'NONE', #122863 ) ;
#33316=CARTESIAN_POINT ( 'NONE',  ( -39.48921356237310221, -27.52281430457082934, 5.000000000000000000 ) ) ;
#33317=ORIENTED_EDGE ( 'NONE', *, *, #44347, .T. ) ;
#33318=FACE_OUTER_BOUND ( 'NONE', #72298, .T. ) ;
#33319=ORIENTED_EDGE ( 'NONE', *, *, #61364, .F. ) ;
#33320=ORIENTED_EDGE ( 'NONE', *, *, #101685, .F. ) ;
#33322=ORIENTED_EDGE ( 'NONE', *, *, #121125, .T. ) ;
#33324=DIRECTION ( 'NONE',  ( -0.3543493200069162685, -0.000000000000000000, -0.9351131265310288487 ) ) ;
#33325=VECTOR ( 'NONE', #66013, 1000.000000000000000 ) ;
#33328=CARTESIAN_POINT ( 'NONE',  ( -24.48921356237309510, -27.52281430457072631, 5.000000000000000000 ) ) ;
#33330=LINE ( 'NONE', #121696, #143130 ) ;
#33331=CARTESIAN_POINT ( 'NONE',  ( 13.49999999999990052, -14.70932175296476352, -11.46312253303840478 ) ) ;
#33332=AXIS2_PLACEMENT_3D ( 'NONE', #116924, #17591, #61860 ) ;
#33333=LINE ( 'NONE', #98536, #118758 ) ;
#33334=CARTESIAN_POINT ( 'NONE',  ( 20.99451991528748707, 28.92564299267952777, 4.000000000000000000 ) ) ;
#33335=EDGE_CURVE ( 'NONE', #103671, #21557, #67068, .T. ) ;
#33336=DIRECTION ( 'NONE',  ( -0.7071067811865487940, 0.7071067811865463515, -0.000000000000000000 ) ) ;
#33337=LINE ( 'NONE', #12240, #100430 ) ;
#33338=EDGE_LOOP ( 'NONE', ( #115845, #15677, #118942, #46294 ) ) ;
#33339=ORIENTED_EDGE ( 'NONE', *, *, #73087, .F. ) ;
#33340=ORIENTED_EDGE ( 'NONE', *, *, #78606, .F. ) ;
#33342=ORIENTED_EDGE ( 'NONE', *, *, #120272, .F. ) ;
#33344=ORIENTED_EDGE ( 'NONE', *, *, #89753, .F. ) ;
#33345=DIRECTION ( 'NONE',  ( -0.7071067811865486830, -0.7071067811865464625, 0.000000000000000000 ) ) ;
#33348=ADVANCED_FACE ( 'NONE', ( #56231 ), #34429, .F. ) ;
#33349=CARTESIAN_POINT ( 'NONE',  ( -28.49999999999980815, 12.43112307739205846, 4.000000000000000000 ) ) ;
#33352=ORIENTED_EDGE ( 'NONE', *, *, #105358, .T. ) ;
#33355=VECTOR ( 'NONE', #48088, 1000.000000000000227 ) ;
#33356=VECTOR ( 'NONE', #78245, 1000.000000000000000 ) ;
#33358=VERTEX_POINT ( 'NONE', #1749 ) ;
#33360=DIRECTION ( 'NONE',  ( 0.7071067811865486830, -0.7071067811865464625, -0.000000000000000000 ) ) ;
#33361=CARTESIAN_POINT ( 'NONE',  ( 33.48921356237309510, -27.52281430457078670, 5.000000000000000000 ) ) ;
#33363=ORIENTED_EDGE ( 'NONE', *, *, #104781, .F. ) ;
#33364=ORIENTED_EDGE ( 'NONE', *, *, #100797, .F. ) ;
#33365=CARTESIAN_POINT ( 'NONE',  ( -4.499999999999968914, -13.91253812416061209, 4.000000000000000000 ) ) ;
#33366=CARTESIAN_POINT ( 'NONE',  ( 57.48921356237308800, -27.52281430457095368, 5.000000000000000000 ) ) ;
#33367=VECTOR ( 'NONE', #22964, 1000.000000000000000 ) ;
#33369=DIRECTION ( 'NONE',  ( 0.7071067811865487940, 0.7071067811865463515, 0.000000000000000000 ) ) ;
#33370=DIRECTION ( 'NONE',  ( -0.000000000000000000, 0.3543493200069153248, 0.9351131265310292928 ) ) ;
#33371=EDGE_CURVE ( 'NONE', #1453, #2022, #56550, .T. ) ;
#33372=EDGE_LOOP ( 'NONE', ( #67497, #2469, #5300, #44123 ) ) ;
#33374=DIRECTION ( 'NONE',  ( -0.7071067811865487940, 0.7071067811865463515, 0.000000000000000000 ) ) ;
#33376=ORIENTED_EDGE ( 'NONE', *, *, #28466, .F. ) ;
#33377=DIRECTION ( 'NONE',  ( 0.6830127018922180770, -0.6830127018922204085, -0.2588190451025213501 ) ) ;
#33378=AXIS2_PLACEMENT_3D ( 'NONE', #60083, #47112, #57965 ) ;
#33379=DIRECTION ( 'NONE',  ( -0.7071067811865487940, 0.7071067811865463515, -0.000000000000000000 ) ) ;
#33380=VERTEX_POINT ( 'NONE', #112696 ) ;
#33381=LINE ( 'NONE', #133380, #76448 ) ;
#33383=EDGE_LOOP ( 'NONE', ( #62836, #142691, #102658, #128839 ) ) ;
#33384=LINE ( 'NONE', #67422, #141999 ) ;
#33387=CARTESIAN_POINT ( 'NONE',  ( -5.999999999999954703, 7.552185695429089130, 5.000000000000000000 ) ) ;
#33388=PLANE ( 'NONE',  #119264 ) ;
#33389=ADVANCED_FACE ( 'NONE', ( #124290 ), #61234, .F. ) ;
#33391=VECTOR ( 'NONE', #73432, 1000.000000000000000 ) ;
#33392=PLANE ( 'NONE',  #41585 ) ;
#33393=ADVANCED_FACE ( 'NONE', ( #50310 ), #116973, .F. ) ;
#33394=CARTESIAN_POINT ( 'NONE',  ( 30.70710678118632941, -12.74070752338415247, 5.000000000000000000 ) ) ;
#33395=DIRECTION ( 'NONE',  ( -0.7071067811865487940, 0.7071067811865463515, 0.000000000000000000 ) ) ;
#33396=DIRECTION ( 'NONE',  ( 0.3543493200069162685, -0.000000000000000000, -0.9351131265310288487 ) ) ;
#33397=DIRECTION ( 'NONE',  ( 0.7071067811865486830, -0.7071067811865464625, -0.000000000000000000 ) ) ;
#33399=FACE_OUTER_BOUND ( 'NONE', #100729, .T. ) ;
#33400=DIRECTION ( 'NONE',  ( -0.7071067811865487940, 0.7071067811865463515, 0.000000000000000000 ) ) ;
#33401=PLANE ( 'NONE',  #4794 ) ;
#33402=DIRECTION ( 'NONE',  ( 0.7071067811865487940, 0.7071067811865463515, 0.000000000000000000 ) ) ;
#33403=EDGE_CURVE ( 'NONE', #96788, #102292, #17643, .T. ) ;
#33404=VERTEX_POINT ( 'NONE', #103240 ) ;
#33405=ADVANCED_FACE ( 'NONE', ( #60494 ), #127132, .F. ) ;
#33406=AXIS2_PLACEMENT_3D ( 'NONE', #30970, #120798, #130281 ) ;
#33407=ORIENTED_EDGE ( 'NONE', *, *, #118076, .T. ) ;
#33410=ORIENTED_EDGE ( 'NONE', *, *, #101611, .F. ) ;
#33412=DIRECTION ( 'NONE',  ( 0.7071067811865486830, -0.7071067811865464625, -0.000000000000000000 ) ) ;
#33413=DIRECTION ( 'NONE',  ( -0.7071067811865486830, 0.7071067811865464625, 0.000000000000000000 ) ) ;
#33414=ORIENTED_EDGE ( 'NONE', *, *, #131857, .F. ) ;
#33415=LINE ( 'NONE', #42844, #106431 ) ;
#33416=EDGE_CURVE ( 'NONE', #140659, #99485, #6034, .T. ) ;
#33417=CARTESIAN_POINT ( 'NONE',  ( -5.999999999999953815, -18.41253812416056945, 4.000000000000000000 ) ) ;
#33418=LINE ( 'NONE', #21786, #2592 ) ;
#33419=ORIENTED_EDGE ( 'NONE', *, *, #38885, .T. ) ;
#33421=DIRECTION ( 'NONE',  ( 1.000000000000000000, 0.000000000000000000, 0.000000000000000000 ) ) ;
#33423=VECTOR ( 'NONE', #80200, 1000.000000000000000 ) ;
#33424=CARTESIAN_POINT ( 'NONE',  ( -34.92500000000001137, 16.80009451602703052, 4.759050581649338696 ) ) ;
#33425=CARTESIAN_POINT ( 'NONE',  ( 32.99999999999977973, -12.41253812416062985, 4.000000000000000000 ) ) ;
#33426=LINE ( 'NONE', #100078, #117111 ) ;
#33427=CARTESIAN_POINT ( 'NONE',  ( 8.483345613589499123, 22.22500000000000142, 4.500000000000000888 ) ) ;
#33429=DIRECTION ( 'NONE',  ( -0.3543493200069162685, -0.000000000000000000, -0.9351131265310288487 ) ) ;
#33430=VECTOR ( 'NONE', #100239, 1000.000000000000000 ) ;
#33432=ORIENTED_EDGE ( 'NONE', *, *, #127993, .F. ) ;
#33435=CARTESIAN_POINT ( 'NONE',  ( 5.207106781186508826, 12.75929247661558996, 5.000000000000000000 ) ) ;
#33437=CARTESIAN_POINT ( 'NONE',  ( 21.70710678118638981, -6.740707523384214639, 5.000000000000000000 ) ) ;
#33438=CARTESIAN_POINT ( 'NONE',  ( 33.48921356237309510, -27.52281430457078670, 5.000000000000000000 ) ) ;
#33442=ORIENTED_EDGE ( 'NONE', *, *, #117938, .T. ) ;
#33444=EDGE_CURVE ( 'NONE', #25651, #82699, #76342, .T. ) ;
#33447=ORIENTED_EDGE ( 'NONE', *, *, #46344, .T. ) ;
#33450=VECTOR ( 'NONE', #112479, 1000.000000000000000 ) ;
#33451=ORIENTED_EDGE ( 'NONE', *, *, #94014, .T. ) ;
#33452=FACE_OUTER_BOUND ( 'NONE', #87969, .T. ) ;
#33453=CARTESIAN_POINT ( 'NONE',  ( -9.793339364578404371, 21.75929247661549581, 4.998822639870701856 ) ) ;
#33454=FACE_OUTER_BOUND ( 'NONE', #24027, .T. ) ;
#33456=ADVANCED_FACE ( 'NONE', ( #108204 ), #19093, .F. ) ;
#33459=VERTEX_POINT ( 'NONE', #62617 ) ;
#33460=FACE_OUTER_BOUND ( 'NONE', #38964, .T. ) ;
#33461=VERTEX_POINT ( 'NONE', #84385 ) ;
#33462=ORIENTED_EDGE ( 'NONE', *, *, #89622, .F. ) ;
#33463=ORIENTED_EDGE ( 'NONE', *, *, #59876, .F. ) ;
#33464=DIRECTION ( 'NONE',  ( -0.6830127018922181881, 0.6830127018922202975, -0.2588190451025214056 ) ) ;
#33466=ORIENTED_EDGE ( 'NONE', *, *, #93592, .F. ) ;
#33467=PLANE ( 'NONE',  #129298 ) ;
#33468=EDGE_CURVE ( 'NONE', #130345, #18115, #120507, .T. ) ;
#33469=CARTESIAN_POINT ( 'NONE',  ( 8.999999999999941380, 8.966399257802168066, 5.000000000000000000 ) ) ;
#33470=FACE_BOUND ( 'NONE', #87450, .T. ) ;
#33471=ORIENTED_EDGE ( 'NONE', *, *, #40194, .F. ) ;
#33472=LINE ( 'NONE', #134928, #62058 ) ;
#33473=EDGE_CURVE ( 'NONE', #108519, #10814, #19798, .T. ) ;
#33474=DIRECTION ( 'NONE',  ( -0.7071067811865486830, 0.7071067811865464625, 0.000000000000000000 ) ) ;
#33475=DIRECTION ( 'NONE',  ( 0.6830127018922181881, 0.6830127018922202975, -0.2588190451025214056 ) ) ;
#33476=EDGE_LOOP ( 'NONE', ( #104052, #28166, #30986, #303 ) ) ;
#33478=VERTEX_POINT ( 'NONE', #42303 ) ;
#33479=EDGE_LOOP ( 'NONE', ( #81194, #75533, #22565 ) ) ;
#33480=LINE ( 'NONE', #113671, #7788 ) ;
#33481=ORIENTED_EDGE ( 'NONE', *, *, #98234, .T. ) ;
#33484=DIRECTION ( 'NONE',  ( 0.6830127018922181881, 0.6830127018922202975, -0.2588190451025214056 ) ) ;
#33485=PLANE ( 'NONE',  #61251 ) ;
#33486=CARTESIAN_POINT ( 'NONE',  ( 20.99999999999984368, -2.904428200921294057, -6.989807076074993297 ) ) ;
#33487=ORIENTED_EDGE ( 'NONE', *, *, #5976, .F. ) ;
#33488=CARTESIAN_POINT ( 'NONE',  ( -13.10362284818588741, 2.655808543615126638, 5.000000000000000000 ) ) ;
#33489=CARTESIAN_POINT ( 'NONE',  ( 9.423278458063483853, 11.25929247661560240, 17.85071094206582387 ) ) ;
#33491=CARTESIAN_POINT ( 'NONE',  ( -3.299744871391591339, -27.71228299555208352, 4.000000000000000000 ) ) ;
#33492=EDGE_CURVE ( 'NONE', #46825, #136452, #7488, .T. ) ;
#33495=DIRECTION ( 'NONE',  ( -0.7071067811865486830, -0.7071067811865464625, 0.000000000000000000 ) ) ;
#33496=EDGE_CURVE ( 'NONE', #103780, #41370, #107526, .T. ) ;
#33497=VERTEX_POINT ( 'NONE', #109670 ) ;
#33498=ORIENTED_EDGE ( 'NONE', *, *, #112427, .F. ) ;
#33499=EDGE_LOOP ( 'NONE', ( #130964, #20560, #20710, #123928 ) ) ;
#33500=DIRECTION ( 'NONE',  ( 0.7071067811865486830, -0.7071067811865464625, -0.000000000000000000 ) ) ;
#33501=PLANE ( 'NONE',  #81519 ) ;
#33502=ORIENTED_EDGE ( 'NONE', *, *, #35035, .F. ) ;
#33503=ORIENTED_EDGE ( 'NONE', *, *, #43858, .T. ) ;
#33504=FACE_OUTER_BOUND ( 'NONE', #130581, .T. ) ;
#33505=EDGE_CURVE ( 'NONE', #967, #4434, #140173, .T. ) ;
#33506=EDGE_CURVE ( 'NONE', #12339, #78479, #21235, .T. ) ;
#33507=DIRECTION ( 'NONE',  ( -0.7071067811865486830, 0.7071067811865464625, 0.000000000000000000 ) ) ;
#33508=ORIENTED_EDGE ( 'NONE', *, *, #44607, .T. ) ;
#33509=CARTESIAN_POINT ( 'NONE',  ( 7.828169399223479985, 6.759292476615645917, 4.000000000000000000 ) ) ;
#33510=AXIS2_PLACEMENT_3D ( 'NONE', #3811, #37209, #137244 ) ;
#33511=DIRECTION ( 'NONE',  ( -0.6830127018922181881, 0.6830127018922202975, -0.2588190451025214056 ) ) ;
#33512=AXIS2_PLACEMENT_3D ( 'NONE', #54449, #122513, #142855 ) ;
#33514=PLANE ( 'NONE',  #124907 ) ;
#33515=ORIENTED_EDGE ( 'NONE', *, *, #47471, .T. ) ;
#33517=EDGE_CURVE ( 'NONE', #119845, #2171, #53132, .T. ) ;
#33518=VECTOR ( 'NONE', #54088, 1000.000000000000000 ) ;
#33519=CARTESIAN_POINT ( 'NONE',  ( -27.79289321881325492, -11.24070752338416490, 5.000000000000000000 ) ) ;
#33520=LINE ( 'NONE', #121895, #79719 ) ;
#33521=LINE ( 'NONE', #111771, #107380 ) ;
#33523=CARTESIAN_POINT ( 'NONE',  ( -21.48921356237309155, -27.52281430457070499, 5.000000000000000000 ) ) ;
#33524=ORIENTED_EDGE ( 'NONE', *, *, #143025, .T. ) ;
#33526=CARTESIAN_POINT ( 'NONE',  ( -31.49999999999977973, 9.052185695429077583, 5.000000000000000000 ) ) ;
#33527=PLANE ( 'NONE',  #88640 ) ;
#33528=CARTESIAN_POINT ( 'NONE',  ( 6.328169399223481761, -21.74070752338406365, 4.000000000000000000 ) ) ;
#33529=EDGE_CURVE ( 'NONE', #28313, #113494, #65494, .T. ) ;
#33530=( BOUNDED_CURVE ( )  B_SPLINE_CURVE ( 3, ( #134399, #131530, #88760, #32220 ),
 .UNSPECIFIED., .F., .F. ) 
 B_SPLINE_CURVE_WITH_KNOTS ( ( 4, 4 ),
 ( 1.964434688349496305, 3.503810798801452187 ),
 .UNSPECIFIED. ) 
 CURVE ( )  GEOMETRIC_REPRESENTATION_ITEM ( )  RATIONAL_B_SPLINE_CURVE ( ( 1.000000000000000000, 0.8120851936182298392, 0.8120851936182298392, 1.000000000000000000 ) ) 
 REPRESENTATION_ITEM ( '' )  );
#33531=ORIENTED_EDGE ( 'NONE', *, *, #29628, .F. ) ;
#33533=DIRECTION ( 'NONE',  ( -0.000000000000000000, 0.3543493200069153248, 0.9351131265310292928 ) ) ;
#33534=DIRECTION ( 'NONE',  ( 0.3543493200069162685, -0.000000000000000000, -0.9351131265310288487 ) ) ;
#33536=DIRECTION ( 'NONE',  ( 0.7071067811865487940, 0.7071067811865463515, -0.000000000000000000 ) ) ;
#33538=CARTESIAN_POINT ( 'NONE',  ( 18.48921356237309510, -27.52281430457068367, 5.000000000000000000 ) ) ;
#33539=ORIENTED_EDGE ( 'NONE', *, *, #102459, .F. ) ;
#33540=FACE_OUTER_BOUND ( 'NONE', #54458, .T. ) ;
#33541=LINE ( 'NONE', #99449, #13784 ) ;
#33542=VERTEX_POINT ( 'NONE', #52425 ) ;
#33543=ORIENTED_EDGE ( 'NONE', *, *, #59822, .T. ) ;
#33544=LINE ( 'NONE', #66160, #61195 ) ;
#33545=VERTEX_POINT ( 'NONE', #85770 ) ;
#33546=AXIS2_PLACEMENT_3D ( 'NONE', #60510, #47516, #71368 ) ;
#33548=VECTOR ( 'NONE', #78919, 1000.000000000000227 ) ;
#33550=CARTESIAN_POINT ( 'NONE',  ( -29.99999999999979039, -1.068876922607804314, 4.000000000000000000 ) ) ;
#33551=DIRECTION ( 'NONE',  ( -0.7071067811865486830, -0.7071067811865464625, 0.000000000000000000 ) ) ;
#33552=ORIENTED_EDGE ( 'NONE', *, *, #102782, .F. ) ;
#33553=VECTOR ( 'NONE', #120964, 1000.000000000000000 ) ;
#33554=EDGE_CURVE ( 'NONE', #69087, #116374, #75631, .T. ) ;
#33555=LINE ( 'NONE', #19070, #65107 ) ;
#33556=DIRECTION ( 'NONE',  ( 1.000000000000000000, 0.000000000000000000, 0.000000000000000000 ) ) ;
#33557=DIRECTION ( 'NONE',  ( -0.6830127018922181881, 0.6830127018922202975, -0.2588190451025214056 ) ) ;
#33558=DIRECTION ( 'NONE',  ( -0.7071067811865487940, 0.7071067811865463515, -0.000000000000000000 ) ) ;
#33560=CARTESIAN_POINT ( 'NONE',  ( 0.000000000000000000, 0.000000000000000000, 5.000000000000000000 ) ) ;
#33563=ORIENTED_EDGE ( 'NONE', *, *, #70497, .T. ) ;
#33564=VERTEX_POINT ( 'NONE', #110940 ) ;
#33566=ORIENTED_EDGE ( 'NONE', *, *, #114654, .T. ) ;
#33567=ORIENTED_EDGE ( 'NONE', *, *, #40754, .F. ) ;
#33568=CARTESIAN_POINT ( 'NONE',  ( -2.700255128608413990, -27.71228299555204089, 4.000000000000000000 ) ) ;
#33569=CARTESIAN_POINT ( 'NONE',  ( -8.206660635421469507, 21.75929247661548516, 4.998822639870715179 ) ) ;
#33570=VERTEX_POINT ( 'NONE', #100814 ) ;
#33571=CARTESIAN_POINT ( 'NONE',  ( -60.18398860626900415, 28.73617430169829490, 5.000000000000000000 ) ) ;
#33572=DIRECTION ( 'NONE',  ( -0.6830127018922180770, -0.6830127018922204085, -0.2588190451025213501 ) ) ;
#33573=DIRECTION ( 'NONE',  ( -0.000000000000000000, 0.3543493200069153248, 0.9351131265310292928 ) ) ;
#33574=EDGE_CURVE ( 'NONE', #31939, #66309, #1466, .T. ) ;
#33575=CARTESIAN_POINT ( 'NONE',  ( -17.99999999999987566, 18.08204922493371214, 0.9627537363045279850 ) ) ;
#33577=ORIENTED_EDGE ( 'NONE', *, *, #67771, .T. ) ;
#33578=EDGE_CURVE ( 'NONE', #8853, #43828, #57340, .T. ) ;
#33579=CARTESIAN_POINT ( 'NONE',  ( 63.48921356237309510, -27.52281430457099631, 5.000000000000000000 ) ) ;
#33581=CARTESIAN_POINT ( 'NONE',  ( 32.99999999999977973, 16.55218569542899942, 5.000000000000000000 ) ) ;
#33582=FACE_OUTER_BOUND ( 'NONE', #100900, .T. ) ;
#33585=CARTESIAN_POINT ( 'NONE',  ( 21.18398860626899349, 28.73617430169802134, 5.000000000000000000 ) ) ;
#33586=PLANE ( 'NONE',  #9033 ) ;
#33587=ORIENTED_EDGE ( 'NONE', *, *, #26202, .T. ) ;
#33588=ORIENTED_EDGE ( 'NONE', *, *, #40410, .F. ) ;
#33590=EDGE_CURVE ( 'NONE', #129048, #78673, #125431, .T. ) ;
#33592=LINE ( 'NONE', #122702, #131829 ) ;
#33593=ORIENTED_EDGE ( 'NONE', *, *, #118180, .F. ) ;
#33594=EDGE_CURVE ( 'NONE', #70001, #23807, #60929, .T. ) ;
#33596=CARTESIAN_POINT ( 'NONE',  ( 0.000000000000000000, 0.000000000000000000, 5.000000000000000000 ) ) ;
#33598=VERTEX_POINT ( 'NONE', #94204 ) ;
#33599=LINE ( 'NONE', #64779, #61897 ) ;
#33601=EDGE_LOOP ( 'NONE', ( #71716, #30536, #95297, #71122 ) ) ;
#33602=EDGE_CURVE ( 'NONE', #27758, #105889, #61663, .T. ) ;
#33603=CARTESIAN_POINT ( 'NONE',  ( 0.000000000000000000, 0.000000000000000000, 5.000000000000000000 ) ) ;
#33604=LINE ( 'NONE', #75661, #63947 ) ;
#33605=LINE ( 'NONE', #45902, #65183 ) ;
#33606=DIRECTION ( 'NONE',  ( 0.7071067811865487940, 0.7071067811865463515, 0.000000000000000000 ) ) ;
#33607=EDGE_LOOP ( 'NONE', ( #104582, #57827, #107517 ) ) ;
#33608=DIRECTION ( 'NONE',  ( -0.000000000000000000, 0.000000000000000000, 1.000000000000000000 ) ) ;
#33611=PLANE ( 'NONE',  #4470 ) ;
#33613=CARTESIAN_POINT ( 'NONE',  ( -34.49999999999974420, -20.94567065516883275, 4.994342998332162331 ) ) ;
#33615=DIRECTION ( 'NONE',  ( -0.000000000000000000, 0.000000000000000000, 1.000000000000000000 ) ) ;
#33616=EDGE_CURVE ( 'NONE', #25257, #95492, #81958, .T. ) ;
#33618=ORIENTED_EDGE ( 'NONE', *, *, #76203, .F. ) ;
#33619=LINE ( 'NONE', #67687, #61561 ) ;
#33622=CARTESIAN_POINT ( 'NONE',  ( -8.816011393731004731, 28.73617430169781173, 5.000000000000000000 ) ) ;
#33623=CARTESIAN_POINT ( 'NONE',  ( 34.92499999999998295, -9.415263340095632927, 16.98967855471611799 ) ) ;
#33624=PLANE ( 'NONE',  #3945 ) ;
#33625=ORIENTED_EDGE ( 'NONE', *, *, #86257, .F. ) ;
#33629=EDGE_LOOP ( 'NONE', ( #52471, #122740, #47197, #32204 ) ) ;
#33630=VECTOR ( 'NONE', #108727, 1000.000000000000000 ) ;
#33632=VERTEX_POINT ( 'NONE', #126145 ) ;
#33633=LINE ( 'NONE', #54662, #139569 ) ;
#33634=CARTESIAN_POINT ( 'NONE',  ( -2.999999999999979128, -12.03360074219761700, 5.000000000000000000 ) ) ;
#33635=DIRECTION ( 'NONE',  ( 0.6830127018922180770, -0.6830127018922204085, -0.2588190451025213501 ) ) ;
#33636=FACE_OUTER_BOUND ( 'NONE', #81293, .T. ) ;
#33637=FACE_BOUND ( 'NONE', #89066, .T. ) ;
#33638=CARTESIAN_POINT ( 'NONE',  ( -24.18398860626899705, 28.73617430169804265, 5.000000000000000000 ) ) ;
#33639=DIRECTION ( 'NONE',  ( -0.6830127018922180770, -0.6830127018922204085, -0.2588190451025213501 ) ) ;
#33640=LINE ( 'NONE', #66965, #136052 ) ;
#33641=PLANE ( 'NONE',  #99068 ) ;
#33642=ORIENTED_EDGE ( 'NONE', *, *, #27567, .T. ) ;
#33643=CARTESIAN_POINT ( 'NONE',  ( -42.29974487139158157, -27.71228299555235708, 4.000000000000000000 ) ) ;
#33645=VERTEX_POINT ( 'NONE', #39134 ) ;
#33646=VECTOR ( 'NONE', #109057, 1000.000000000000000 ) ;
#33647=VECTOR ( 'NONE', #106736, 1000.000000000000227 ) ;
#33648=ORIENTED_EDGE ( 'NONE', *, *, #80992, .F. ) ;
#33650=ORIENTED_EDGE ( 'NONE', *, *, #88380, .F. ) ;
#33652=CARTESIAN_POINT ( 'NONE',  ( -6.183988606268994381, 28.73617430169791476, 5.000000000000000000 ) ) ;
#33653=EDGE_CURVE ( 'NONE', #91708, #3709, #38418, .T. ) ;
#33654=EDGE_LOOP ( 'NONE', ( #34654, #149, #92124, #119468 ) ) ;
#33655=CARTESIAN_POINT ( 'NONE',  ( 27.48921356237309155, -27.52281430457074762, 5.000000000000000000 ) ) ;
#33656=DIRECTION ( 'NONE',  ( -0.7071067811865486830, -0.7071067811865464625, -0.000000000000000000 ) ) ;
#33657=CARTESIAN_POINT ( 'NONE',  ( -34.92500000000001137, 0.6624618758389808626, 4.000000000000000000 ) ) ;
#33658=LINE ( 'NONE', #79329, #96460 ) ;
#33659=FACE_OUTER_BOUND ( 'NONE', #121179, .T. ) ;
#33660=DIRECTION ( 'NONE',  ( -0.7071067811865486830, -0.7071067811865464625, 0.000000000000000000 ) ) ;
#33661=CARTESIAN_POINT ( 'NONE',  ( -26.99451991528749417, 28.92564299267956685, 4.000000000000000000 ) ) ;
#33662=FACE_OUTER_BOUND ( 'NONE', #107099, .T. ) ;
#33663=VERTEX_POINT ( 'NONE', #93508 ) ;
#33664=FACE_OUTER_BOUND ( 'NONE', #97464, .T. ) ;
#33665=ORIENTED_EDGE ( 'NONE', *, *, #108560, .T. ) ;
#33666=FACE_OUTER_BOUND ( 'NONE', #83947, .T. ) ;
#33667=CARTESIAN_POINT ( 'NONE',  ( 12.18398860626900060, 28.73617430169795739, 5.000000000000000000 ) ) ;
#33668=ORIENTED_EDGE ( 'NONE', *, *, #62620, .F. ) ;
#33669=ORIENTED_EDGE ( 'NONE', *, *, #133650, .T. ) ;
#33670=ORIENTED_EDGE ( 'NONE', *, *, #11409, .F. ) ;
#33672=EDGE_CURVE ( 'NONE', #89696, #50223, #36971, .T. ) ;
#33675=CARTESIAN_POINT ( 'NONE',  ( 20.70025512860841133, -27.71228299555191654, 4.000000000000000000 ) ) ;
#33676=EDGE_CURVE ( 'NONE', #106936, #60182, #81226, .T. ) ;
#33680=VERTEX_POINT ( 'NONE', #71774 ) ;
#33682=CARTESIAN_POINT ( 'NONE',  ( -34.92500000000001137, -4.168643983631880268, 15.00153835162127969 ) ) ;
#33683=LINE ( 'NONE', #45286, #93742 ) ;
#33684=CARTESIAN_POINT ( 'NONE',  ( 0.000000000000000000, 0.000000000000000000, 5.000000000000000000 ) ) ;
#33685=ORIENTED_EDGE ( 'NONE', *, *, #132604, .F. ) ;
#33686=ORIENTED_EDGE ( 'NONE', *, *, #92256, .T. ) ;
#33688=FACE_OUTER_BOUND ( 'NONE', #24588, .T. ) ;
#33689=DIRECTION ( 'NONE',  ( 0.7071067811865487940, 0.7071067811865463515, 0.000000000000000000 ) ) ;
#33690=ADVANCED_FACE ( 'NONE', ( #72355 ), #93344, .F. ) ;
#33691=ORIENTED_EDGE ( 'NONE', *, *, #136946, .T. ) ;
#33693=CARTESIAN_POINT ( 'NONE',  ( 34.45011844616453800, -14.99769585840590302, 5.000000000000001776 ) ) ;
#33694=ORIENTED_EDGE ( 'NONE', *, *, #106933, .F. ) ;
#33696=PLANE ( 'NONE',  #135092 ) ;
#33697=EDGE_CURVE ( 'NONE', #38602, #141315, #18604, .T. ) ;
#33698=FACE_OUTER_BOUND ( 'NONE', #141410, .T. ) ;
#33699=LINE ( 'NONE', #100371, #42436 ) ;
#33700=LINE ( 'NONE', #1713, #28298 ) ;
#33702=CARTESIAN_POINT ( 'NONE',  ( -2.381615093980022024, -2.240707523384260824, 13.37739548510239906 ) ) ;
#33706=EDGE_CURVE ( 'NONE', #137770, #23390, #104184, .T. ) ;
#33710=( BOUNDED_CURVE ( )  B_SPLINE_CURVE ( 3, ( #66206, #101664, #90819, #45891 ),
 .UNSPECIFIED., .F., .T. ) 
 B_SPLINE_CURVE_WITH_KNOTS ( ( 4, 4 ),
 ( 1.208578181583249256, 1.359146454359418055 ),
 .UNSPECIFIED. ) 
 CURVE ( )  GEOMETRIC_REPRESENTATION_ITEM ( )  RATIONAL_B_SPLINE_CURVE ( ( 1.000000000000000000, 0.9981116584018960847, 0.9981116584018960847, 1.000000000000000000 ) ) 
 REPRESENTATION_ITEM ( '' )  );
#33713=FACE_OUTER_BOUND ( 'NONE', #50367, .T. ) ;
#33714=ORIENTED_EDGE ( 'NONE', *, *, #95553, .F. ) ;
#33715=DIRECTION ( 'NONE',  ( 0.3543493200069162685, -0.000000000000000000, -0.9351131265310288487 ) ) ;
#33716=LINE ( 'NONE', #32271, #129825 ) ;
#33718=VECTOR ( 'NONE', #112049, 1000.000000000000000 ) ;
#33719=ORIENTED_EDGE ( 'NONE', *, *, #52016, .T. ) ;
#33720=EDGE_CURVE ( 'NONE', #45460, #35930, #125988, .T. ) ;
#33721=PLANE ( 'NONE',  #106545 ) ;
#33723=FACE_OUTER_BOUND ( 'NONE', #103861, .T. ) ;
#33725=CARTESIAN_POINT ( 'NONE',  ( 66.48921356237309510, -27.52281430457101763, 5.000000000000000000 ) ) ;
#33727=FACE_OUTER_BOUND ( 'NONE', #110644, .T. ) ;
#33728=ADVANCED_FACE ( 'NONE', ( #27348 ), #17210, .F. ) ;
#33729=EDGE_CURVE ( 'NONE', #21534, #24725, #73726, .T. ) ;
#33730=CARTESIAN_POINT ( 'NONE',  ( -30.48921356237309510, -27.52281430457076894, 5.000000000000000000 ) ) ;
#33731=VECTOR ( 'NONE', #54946, 999.9999999999998863 ) ;
#33732=LINE ( 'NONE', #87380, #64955 ) ;
#33733=ORIENTED_EDGE ( 'NONE', *, *, #47607, .F. ) ;
#33735=ORIENTED_EDGE ( 'NONE', *, *, #143397, .F. ) ;
#33736=CARTESIAN_POINT ( 'NONE',  ( -4.828169399223495084, -14.24070752338413648, 4.000000000000000000 ) ) ;
#33737=FACE_OUTER_BOUND ( 'NONE', #44441, .T. ) ;
#33738=EDGE_CURVE ( 'NONE', #55203, #77465, #127388, .T. ) ;
#33739=DIRECTION ( 'NONE',  ( 0.7071067811865486830, -0.7071067811865464625, -0.000000000000000000 ) ) ;
#33740=PLANE ( 'NONE',  #76660 ) ;
#33741=CARTESIAN_POINT ( 'NONE',  ( 8.510786437626906675, -27.52281430457049183, 5.000000000000000000 ) ) ;
#33742=EDGE_CURVE ( 'NONE', #78506, #1174, #83187, .T. ) ;
#33743=CARTESIAN_POINT ( 'NONE',  ( 51.29974487139158867, -27.71228299555242103, 4.000000000000000000 ) ) ;
#33744=CARTESIAN_POINT ( 'NONE',  ( -21.18398860626899349, 28.73617430169802134, 5.000000000000000000 ) ) ;
#33745=ORIENTED_EDGE ( 'NONE', *, *, #62331, .F. ) ;
#33746=EDGE_LOOP ( 'NONE', ( #138608, #141589, #121346, #111903 ) ) ;
#33747=DIRECTION ( 'NONE',  ( 0.7071067811865486830, -0.7071067811865464625, -0.000000000000000000 ) ) ;
#33748=LINE ( 'NONE', #78661, #130684 ) ;
#33749=VECTOR ( 'NONE', #120749, 1000.000000000000000 ) ;
#33750=CARTESIAN_POINT ( 'NONE',  ( -28.82816939922333077, -17.24070752338409918, 4.000000000000000000 ) ) ;
#33752=CARTESIAN_POINT ( 'NONE',  ( -12.18398860626900060, 28.73617430169795739, 5.000000000000000000 ) ) ;
#33753=AXIS2_PLACEMENT_3D ( 'NONE', #36585, #34460, #3236 ) ;
#33754=CARTESIAN_POINT ( 'NONE',  ( 66.18398860626901126, 28.73617430169833753, 5.000000000000000000 ) ) ;
#33755=ORIENTED_EDGE ( 'NONE', *, *, #94951, .F. ) ;
#33757=AXIS2_PLACEMENT_3D ( 'NONE', #4157, #123175, #138153 ) ;
#33758=EDGE_CURVE ( 'NONE', #76267, #102238, #60763, .T. ) ;
#33759=FACE_OUTER_BOUND ( 'NONE', #133690, .T. ) ;
#33760=FACE_OUTER_BOUND ( 'NONE', #22317, .T. ) ;
#33762=VECTOR ( 'NONE', #98422, 1000.000000000000000 ) ;
#33763=VERTEX_POINT ( 'NONE', #117907 ) ;
#33764=EDGE_CURVE ( 'NONE', #16747, #84400, #28087, .T. ) ;
#33765=LINE ( 'NONE', #67091, #49129 ) ;
#33770=EDGE_LOOP ( 'NONE', ( #135593, #107271, #48198, #70843 ) ) ;
#33771=DIRECTION ( 'NONE',  ( -0.7071067811865486830, -0.7071067811865464625, -0.000000000000000000 ) ) ;
#33772=DIRECTION ( 'NONE',  ( 1.000000000000000000, 0.000000000000000000, 0.000000000000000000 ) ) ;
#33774=CARTESIAN_POINT ( 'NONE',  ( -36.48921356237310221, -27.52281430457080802, 5.000000000000000000 ) ) ;
#33777=VERTEX_POINT ( 'NONE', #107066 ) ;
#33779=CARTESIAN_POINT ( 'NONE',  ( 57.18398860626899705, 28.73617430169827358, 5.000000000000000000 ) ) ;
#33780=LINE ( 'NONE', #69253, #72615 ) ;
#33783=ORIENTED_EDGE ( 'NONE', *, *, #117897, .T. ) ;
#33785=ORIENTED_EDGE ( 'NONE', *, *, #40253, .T. ) ;
#33786=DIRECTION ( 'NONE',  ( 0.7071067811865487940, 0.7071067811865463515, -0.000000000000000000 ) ) ;
#33788=DIRECTION ( 'NONE',  ( 0.000000000000000000, 0.000000000000000000, 1.000000000000000000 ) ) ;
#33789=CARTESIAN_POINT ( 'NONE',  ( -26.67183060077627488, 2.259292476615697876, 4.000000000000000000 ) ) ;
#33790=DIRECTION ( 'NONE',  ( 0.7071067811865487940, -0.7071067811865463515, 0.000000000000000000 ) ) ;
#33791=VERTEX_POINT ( 'NONE', #15724 ) ;
#33792=EDGE_LOOP ( 'NONE', ( #64143, #102380, #29702, #115496, #91795, #28090 ) ) ;
#33793=DIRECTION ( 'NONE',  ( 0.7071067811865487940, 0.7071067811865463515, -0.000000000000000000 ) ) ;
#33795=ORIENTED_EDGE ( 'NONE', *, *, #16352, .F. ) ;
#33796=LINE ( 'NONE', #108432, #67589 ) ;
#33798=DIRECTION ( 'NONE',  ( 0.7071067811865487940, -0.7071067811865463515, 0.000000000000000000 ) ) ;
#33800=FACE_BOUND ( 'NONE', #30266, .T. ) ;
#33801=LINE ( 'NONE', #57703, #17719 ) ;
#33802=LINE ( 'NONE', #46859, #69836 ) ;
#33803=CARTESIAN_POINT ( 'NONE',  ( -27.29974487139158512, -27.71228299555225405, 4.000000000000000000 ) ) ;
#33805=DIRECTION ( 'NONE',  ( -0.7071067811865486830, 0.7071067811865464625, 0.000000000000000000 ) ) ;
#33806=CIRCLE ( 'NONE', #142565, 0.5000000000000004441 ) ;
#33807=EDGE_LOOP ( 'NONE', ( #100248, #81552, #101357 ) ) ;
#33808=ORIENTED_EDGE ( 'NONE', *, *, #47299, .T. ) ;
#33812=LINE ( 'NONE', #67144, #92888 ) ;
#33813=ORIENTED_EDGE ( 'NONE', *, *, #99554, .T. ) ;
#33814=EDGE_CURVE ( 'NONE', #110456, #89877, #86037, .T. ) ;
#33817=LINE ( 'NONE', #46129, #7728 ) ;
#33818=ORIENTED_EDGE ( 'NONE', *, *, #123570, .F. ) ;
#33819=LINE ( 'NONE', #134565, #131698 ) ;
#33822=VECTOR ( 'NONE', #98092, 1000.000000000000000 ) ;
#33823=CARTESIAN_POINT ( 'NONE',  ( 17.99999999999987921, 11.96639925780213254, 5.000000000000000000 ) ) ;
#33824=CARTESIAN_POINT ( 'NONE',  ( 32.52487387214934245, 14.25929247661556865, 9.797011795316713290 ) ) ;
#33825=CARTESIAN_POINT ( 'NONE',  ( 9.722814304570524868, -21.72500000000000497, 5.000000000000000000 ) ) ;
#33826=CARTESIAN_POINT ( 'NONE',  ( 30.18398860626900060, 28.73617430169808173, 5.000000000000000000 ) ) ;
#33827=ORIENTED_EDGE ( 'NONE', *, *, #13152, .F. ) ;
#33828=DIRECTION ( 'NONE',  ( -0.6830127018922181881, 0.6830127018922202975, -0.2588190451025214056 ) ) ;
#33829=CARTESIAN_POINT ( 'NONE',  ( 6.183988606268994381, 28.73617430169791476, 5.000000000000000000 ) ) ;
#33830=EDGE_CURVE ( 'NONE', #7428, #35701, #54857, .T. ) ;
#33831=VERTEX_POINT ( 'NONE', #119349 ) ;
#33832=ORIENTED_EDGE ( 'NONE', *, *, #36171, .F. ) ;
#33833=ADVANCED_FACE ( 'NONE', ( #43266 ), #8427, .T. ) ;
#33834=EDGE_CURVE ( 'NONE', #93386, #59760, #30220, .T. ) ;
#33835=ORIENTED_EDGE ( 'NONE', *, *, #90482, .T. ) ;
#33837=EDGE_LOOP ( 'NONE', ( #120753, #32066, #57331, #89782 ) ) ;
#33839=EDGE_CURVE ( 'NONE', #81231, #71971, #107765, .T. ) ;
#33840=EDGE_CURVE ( 'NONE', #116493, #86617, #9133, .T. ) ;
#33841=DIRECTION ( 'NONE',  ( 0.6830127018922180770, -0.6830127018922204085, -0.2588190451025213501 ) ) ;
#33842=VECTOR ( 'NONE', #99517, 1000.000000000000000 ) ;
#33845=DIRECTION ( 'NONE',  ( 0.7071067811865486830, -0.7071067811865464625, -0.000000000000000000 ) ) ;
#33847=ADVANCED_FACE ( 'NONE', ( #55566 ), #88191, .F. ) ;
#33849=DIRECTION ( 'NONE',  ( 0.7071067811865486830, -0.7071067811865464625, -0.000000000000000000 ) ) ;
#33850=AXIS2_PLACEMENT_3D ( 'NONE', #103589, #47156, #68871 ) ;
#33851=CARTESIAN_POINT ( 'NONE',  ( 2.510786437626908008, -27.52281430457053446, 5.000000000000000000 ) ) ;
#33852=ORIENTED_EDGE ( 'NONE', *, *, #20937, .F. ) ;
#33853=CYLINDRICAL_SURFACE ( 'NONE', #30694, 0.5000000000000000000 ) ;
#33854=DIRECTION ( 'NONE',  ( 1.000000000000000000, -0.000000000000000000, -0.000000000000000000 ) ) ;
#33857=LINE ( 'NONE', #22919, #89770 ) ;
#33858=VERTEX_POINT ( 'NONE', #130275 ) ;
#33859=ORIENTED_EDGE ( 'NONE', *, *, #53076, .F. ) ;
#33862=CARTESIAN_POINT ( 'NONE',  ( -33.18398860626899705, 28.73617430169810305, 5.000000000000000000 ) ) ;
#33863=FACE_OUTER_BOUND ( 'NONE', #30961, .T. ) ;
#33864=PLANE ( 'NONE',  #99769 ) ;
#33865=ORIENTED_EDGE ( 'NONE', *, *, #30070, .F. ) ;
#33866=ADVANCED_FACE ( 'NONE', ( #141870 ), #21502, .F. ) ;
#33869=PLANE ( 'NONE',  #85413 ) ;
#33871=ORIENTED_EDGE ( 'NONE', *, *, #68244, .F. ) ;
#33872=ORIENTED_EDGE ( 'NONE', *, *, #75182, .T. ) ;
#33873=EDGE_CURVE ( 'NONE', #85530, #103515, #110612, .T. ) ;
#33874=VERTEX_POINT ( 'NONE', #65760 ) ;
#33877=VECTOR ( 'NONE', #59961, 1000.000000000000000 ) ;
#33878=CARTESIAN_POINT ( 'NONE',  ( -36.29974487139159578, -27.71228299555231445, 4.000000000000000000 ) ) ;
#33879=LINE ( 'NONE', #78098, #55236 ) ;
#33880=EDGE_CURVE ( 'NONE', #104041, #122724, #86977, .T. ) ;
#33881=DIRECTION ( 'NONE',  ( 0.3543493200069164351, 2.781805975412904658E-17, -0.9351131265310288487 ) ) ;
#33882=LINE ( 'NONE', #57079, #88907 ) ;
#33883=DIRECTION ( 'NONE',  ( -0.3543493200069163240, 0.000000000000000000, -0.9351131265310288487 ) ) ;
#33884=CARTESIAN_POINT ( 'NONE',  ( -28.49999999999980460, 10.46639925780215563, 5.000000000000000000 ) ) ;
#33885=EDGE_CURVE ( 'NONE', #3157, #100719, #130988, .T. ) ;
#33886=ORIENTED_EDGE ( 'NONE', *, *, #13522, .T. ) ;
#33887=CARTESIAN_POINT ( 'NONE',  ( 17.99451991528748351, 28.92564299267950645, 4.000000000000000000 ) ) ;
#33888=AXIS2_PLACEMENT_3D ( 'NONE', #22781, #88096, #130906 ) ;
#33889=ORIENTED_EDGE ( 'NONE', *, *, #85839, .T. ) ;
#33891=ORIENTED_EDGE ( 'NONE', *, *, #74699, .F. ) ;
#33892=EDGE_CURVE ( 'NONE', #19670, #21326, #120792, .T. ) ;
#33893=EDGE_CURVE ( 'NONE', #79777, #140721, #33130, .T. ) ;
#33894=DIRECTION ( 'NONE',  ( -0.7071067811865486830, -0.7071067811865464625, 0.000000000000000000 ) ) ;
#33895=CARTESIAN_POINT ( 'NONE',  ( -23.99999999999983302, 7.007997736742422212, -8.085015511992168058 ) ) ;
#33896=ORIENTED_EDGE ( 'NONE', *, *, #75901, .F. ) ;
#33897=CARTESIAN_POINT ( 'NONE',  ( 22.17183060077631396, 12.75929247661558996, 4.000000000000000000 ) ) ;
#33900=VERTEX_POINT ( 'NONE', #54165 ) ;
#33901=CARTESIAN_POINT ( 'NONE',  ( 34.42499999999998295, 16.54139925780187781, 5.000000000000000000 ) ) ;
#33902=ORIENTED_EDGE ( 'NONE', *, *, #115834, .T. ) ;
#33904=LINE ( 'NONE', #121595, #66110 ) ;
#33905=AXIS2_PLACEMENT_3D ( 'NONE', #19881, #97437, #7573 ) ;
#33908=LINE ( 'NONE', #68001, #57877 ) ;
#33910=EDGE_CURVE ( 'NONE', #133767, #87366, #143265, .T. ) ;
#33911=LINE ( 'NONE', #9232, #109747 ) ;
#33912=LINE ( 'NONE', #1929, #129454 ) ;
#33914=DIRECTION ( 'NONE',  ( 0.6830127018922181881, 0.6830127018922202975, -0.2588190451025214056 ) ) ;
#33915=LINE ( 'NONE', #67250, #79093 ) ;
#33916=PLANE ( 'NONE',  #105717 ) ;
#33917=ORIENTED_EDGE ( 'NONE', *, *, #54022, .F. ) ;
#33920=CARTESIAN_POINT ( 'NONE',  ( 0.000000000000000000, 0.000000000000000000, 5.000000000000000000 ) ) ;
#33921=VERTEX_POINT ( 'NONE', #85297 ) ;
#33924=DIRECTION ( 'NONE',  ( -0.6830127018922180770, -0.6830127018922204085, -0.2588190451025213501 ) ) ;
#33925=CYLINDRICAL_SURFACE ( 'NONE', #62296, 0.5000000000000004441 ) ;
#33926=CARTESIAN_POINT ( 'NONE',  ( 28.49999999999980815, -17.91344420646039737, 1.358650452708529022 ) ) ;
#33930=CARTESIAN_POINT ( 'NONE',  ( 29.99999999999978328, -6.033600742197672950, 5.000000000000000000 ) ) ;
#33931=PLANE ( 'NONE',  #32688 ) ;
#33932=EDGE_CURVE ( 'NONE', #60350, #133314, #114204, .T. ) ;
#33933=VECTOR ( 'NONE', #130241, 1000.000000000000227 ) ;
#33934=LINE ( 'NONE', #13564, #91090 ) ;
#33935=ADVANCED_FACE ( 'NONE', ( #88920 ), #14175, .T. ) ;
#33936=LINE ( 'NONE', #89040, #56814 ) ;
#33939=CARTESIAN_POINT ( 'NONE',  ( 21.29974487139158512, -27.71228299555221142, 4.000000000000000000 ) ) ;
#33940=DIRECTION ( 'NONE',  ( 0.7071067811865486830, -0.7071067811865464625, -0.000000000000000000 ) ) ;
#33941=FACE_OUTER_BOUND ( 'NONE', #66713, .T. ) ;
#33942=VECTOR ( 'NONE', #14331, 1000.000000000000000 ) ;
#33943=DIRECTION ( 'NONE',  ( -0.7071067811865486830, -0.7071067811865464625, 0.000000000000000000 ) ) ;
#33944=VECTOR ( 'NONE', #76401, 1000.000000000000000 ) ;
#33945=VERTEX_POINT ( 'NONE', #14889 ) ;
#33946=EDGE_CURVE ( 'NONE', #46830, #48007, #57010, .T. ) ;
#33947=ORIENTED_EDGE ( 'NONE', *, *, #130170, .T. ) ;
#33948=EDGE_LOOP ( 'NONE', ( #71376, #118201, #61395, #137816, #10196, #100838 ) ) ;
#33949=AXIS2_PLACEMENT_3D ( 'NONE', #101506, #2159, #34132 ) ;
#33951=EDGE_LOOP ( 'NONE', ( #660, #72896, #102332, #61489 ) ) ;
#33953=CARTESIAN_POINT ( 'NONE',  ( 18.32816939922340183, 11.25929247661560595, 4.000000000000000000 ) ) ;
#33954=DIRECTION ( 'NONE',  ( -0.000000000000000000, -1.000000000000000000, -0.000000000000000000 ) ) ;
#33956=ORIENTED_EDGE ( 'NONE', *, *, #95935, .F. ) ;
#33958=CARTESIAN_POINT ( 'NONE',  ( 24.61838490601981988, -2.240707523384257716, 13.37739548510233689 ) ) ;
#33959=EDGE_CURVE ( 'NONE', #71690, #63474, #135282, .T. ) ;
#33960=CARTESIAN_POINT ( 'NONE',  ( 29.67183060077627133, -3.740707523384236399, 4.000000000000000000 ) ) ;
#33962=EDGE_CURVE ( 'NONE', #81346, #10533, #18355, .T. ) ;
#33963=ORIENTED_EDGE ( 'NONE', *, *, #2838, .T. ) ;
#33964=CARTESIAN_POINT ( 'NONE',  ( 5.999999999999974243, 17.58746187583906817, 4.000000000000000000 ) ) ;
#33966=VERTEX_POINT ( 'NONE', #36639 ) ;
#33967=ORIENTED_EDGE ( 'NONE', *, *, #55450, .T. ) ;
#33968=CARTESIAN_POINT ( 'NONE',  ( -0.005480084712502889671, 28.92564299267938210, 4.000000000000000000 ) ) ;
#33971=DIRECTION ( 'NONE',  ( 0.7071067811865486830, -0.7071067811865464625, -0.000000000000000000 ) ) ;
#33972=CARTESIAN_POINT ( 'NONE',  ( 1.190181675744472756, -18.74070752338409562, 7.910009926591503593 ) ) ;
#33973=DIRECTION ( 'NONE',  ( 0.7071067811865487940, 0.7071067811865463515, 0.000000000000000000 ) ) ;
#33975=ORIENTED_EDGE ( 'NONE', *, *, #66068, .T. ) ;
#33976=VERTEX_POINT ( 'NONE', #70042 ) ;
#33978=EDGE_LOOP ( 'NONE', ( #143441, #95928, #12136, #22198 ) ) ;
#33979=EDGE_LOOP ( 'NONE', ( #91382, #58329, #92180, #1827 ) ) ;
#33980=VECTOR ( 'NONE', #39288, 999.9999999999998863 ) ;
#33981=DIRECTION ( 'NONE',  ( -0.6830127018922181881, 0.6830127018922202975, -0.2588190451025214056 ) ) ;
#33982=ORIENTED_EDGE ( 'NONE', *, *, #55937, .T. ) ;
#33983=FACE_OUTER_BOUND ( 'NONE', #126204, .T. ) ;
#33984=LINE ( 'NONE', #102813, #21668 ) ;
#33985=CARTESIAN_POINT ( 'NONE',  ( -9.489213562373095101, -27.52281430457062328, 5.000000000000000000 ) ) ;
#33986=VECTOR ( 'NONE', #19085, 999.9999999999998863 ) ;
#33987=DIRECTION ( 'NONE',  ( 1.000000000000000000, -0.000000000000000000, -0.000000000000000000 ) ) ;
#33988=CARTESIAN_POINT ( 'NONE',  ( 12.61838490601988383, -2.240707523384260824, 13.37739548510236531 ) ) ;
#33989=EDGE_LOOP ( 'NONE', ( #50505, #39261, #70062, #74442 ) ) ;
#33990=VECTOR ( 'NONE', #142735, 1000.000000000000000 ) ;
#33991=VERTEX_POINT ( 'NONE', #112780 ) ;
#33993=ORIENTED_EDGE ( 'NONE', *, *, #12597, .T. ) ;
#33994=DIRECTION ( 'NONE',  ( -0.6830127018922181881, 0.6830127018922202975, -0.2588190451025214056 ) ) ;
#33995=EDGE_CURVE ( 'NONE', #37390, #34938, #102642, .T. ) ;
#33997=LINE ( 'NONE', #23070, #69021 ) ;
#33998=ORIENTED_EDGE ( 'NONE', *, *, #43951, .T. ) ;
#33999=ORIENTED_EDGE ( 'NONE', *, *, #107848, .F. ) ;
#34001=EDGE_CURVE ( 'NONE', #1472, #19682, #46878, .T. ) ;
#34005=LINE ( 'NONE', #78226, #104376 ) ;
#34007=LINE ( 'NONE', #122411, #51849 ) ;
#34008=EDGE_CURVE ( 'NONE', #8278, #121029, #2568, .T. ) ;
#34009=AXIS2_PLACEMENT_3D ( 'NONE', #7552, #109738, #108270 ) ;
#34011=PLANE ( 'NONE',  #123829 ) ;
#34014=CARTESIAN_POINT ( 'NONE',  ( -28.28119340046980668, 22.22500000000000142, 2.482413320905432208 ) ) ;
#34015=VECTOR ( 'NONE', #98783, 999.9999999999998863 ) ;
#34016=FACE_OUTER_BOUND ( 'NONE', #46656, .T. ) ;
#34018=LINE ( 'NONE', #131893, #47021 ) ;
#34019=DIRECTION ( 'NONE',  ( -0.7071067811865486830, 0.7071067811865464625, 0.000000000000000000 ) ) ;
#34021=ORIENTED_EDGE ( 'NONE', *, *, #70429, .F. ) ;
#34022=DIRECTION ( 'NONE',  ( 0.7071067811865487940, 0.7071067811865463515, -0.000000000000000000 ) ) ;
#34023=CARTESIAN_POINT ( 'NONE',  ( 34.47516574401890921, 1.490517612115608737, 4.998110765256834398 ) ) ;
#34024=LINE ( 'NONE', #10790, #37935 ) ;
#34025=ORIENTED_EDGE ( 'NONE', *, *, #114167, .T. ) ;
#34026=EDGE_LOOP ( 'NONE', ( #40884, #54307, #99274, #34893 ) ) ;
#34027=EDGE_LOOP ( 'NONE', ( #140288, #65847, #132623, #79089 ) ) ;
#34028=LINE ( 'NONE', #88411, #72699 ) ;
#34029=ORIENTED_EDGE ( 'NONE', *, *, #53996, .F. ) ;
#34031=DIRECTION ( 'NONE',  ( 4.681814790819592407E-17, 0.3543493200069153248, 0.9351131265310292928 ) ) ;
#34032=DIRECTION ( 'NONE',  ( 0.7071067811865487940, -0.7071067811865463515, 0.000000000000000000 ) ) ;
#34033=ADVANCED_FACE ( 'NONE', ( #67903 ), #112088, .F. ) ;
#34034=VECTOR ( 'NONE', #23417, 1000.000000000000000 ) ;
#34035=CARTESIAN_POINT ( 'NONE',  ( -0.4892135623730947680, -27.52281430457055578, 5.000000000000000000 ) ) ;
#34036=CARTESIAN_POINT ( 'NONE',  ( -39.48921356237310221, -27.52281430457082934, 5.000000000000000000 ) ) ;
#34037=VERTEX_POINT ( 'NONE', #128658 ) ;
#34039=ORIENTED_EDGE ( 'NONE', *, *, #120554, .T. ) ;
#34040=EDGE_CURVE ( 'NONE', #23445, #88587, #15563, .T. ) ;
#34041=VECTOR ( 'NONE', #116684, 1000.000000000000000 ) ;
#34042=LINE ( 'NONE', #2807, #139472 ) ;
#34045=ORIENTED_EDGE ( 'NONE', *, *, #57904, .F. ) ;
#34048=DIRECTION ( 'NONE',  ( 0.6830127018922181881, 0.6830127018922202975, -0.2588190451025214056 ) ) ;
#34050=VECTOR ( 'NONE', #100621, 999.9999999999998863 ) ;
#34051=ORIENTED_EDGE ( 'NONE', *, *, #107751, .F. ) ;
#34053=DIRECTION ( 'NONE',  ( -0.000000000000000000, 0.3543493200069153248, 0.9351131265310292928 ) ) ;
#34054=DIRECTION ( 'NONE',  ( -0.6830127018922180770, -0.6830127018922204085, -0.2588190451025213501 ) ) ;
#34056=AXIS2_PLACEMENT_3D ( 'NONE', #118977, #8736, #40035 ) ;
#34057=LINE ( 'NONE', #133366, #19541 ) ;
#34058=DIRECTION ( 'NONE',  ( 0.7071067811865486830, -0.7071067811865464625, -0.000000000000000000 ) ) ;
#34059=ORIENTED_EDGE ( 'NONE', *, *, #55998, .F. ) ;
#34061=DIRECTION ( 'NONE',  ( -0.3543493200069162685, -0.000000000000000000, -0.9351131265310288487 ) ) ;
#34062=LINE ( 'NONE', #110154, #55814 ) ;
#34063=EDGE_CURVE ( 'NONE', #52412, #98565, #126496, .T. ) ;
#34064=EDGE_LOOP ( 'NONE', ( #13898, #55584, #130258, #11617 ) ) ;
#34066=FACE_OUTER_BOUND ( 'NONE', #48694, .T. ) ;
#34067=EDGE_LOOP ( 'NONE', ( #74543, #33963, #6957, #32531 ) ) ;
#34068=EDGE_CURVE ( 'NONE', #33303, #40492, #38799, .T. ) ;
#34069=CARTESIAN_POINT ( 'NONE',  ( -19.49999999999985434, 13.46639925780212366, 5.000000000000000000 ) ) ;
#34070=ORIENTED_EDGE ( 'NONE', *, *, #49723, .F. ) ;
#34071=ORIENTED_EDGE ( 'NONE', *, *, #114794, .F. ) ;
#34072=DIRECTION ( 'NONE',  ( 0.6830127018922181881, 0.6830127018922202975, -0.2588190451025214056 ) ) ;
#34073=DIRECTION ( 'NONE',  ( -0.7071067811865486830, -0.7071067811865464625, 0.000000000000000000 ) ) ;
#34074=AXIS2_PLACEMENT_3D ( 'NONE', #122433, #99992, #26000 ) ;
#34075=ORIENTED_EDGE ( 'NONE', *, *, #63758, .F. ) ;
#34076=CARTESIAN_POINT ( 'NONE',  ( 34.92499999999998295, -17.14387692260740792, 4.000000000000000000 ) ) ;
#34077=ADVANCED_FACE ( 'NONE', ( #81611 ), #127967, .T. ) ;
#34078=PLANE ( 'NONE',  #3453 ) ;
#34079=AXIS2_PLACEMENT_3D ( 'NONE', #72723, #126325, #127026 ) ;
#34080=CARTESIAN_POINT ( 'NONE',  ( -10.17183060077640278, 15.75929247661555976, 4.000000000000000000 ) ) ;
#34081=( BOUNDED_CURVE ( )  B_SPLINE_CURVE ( 3, ( #120906, #99131, #68018, #143374 ),
 .UNSPECIFIED., .F., .T. ) 
 B_SPLINE_CURVE_WITH_KNOTS ( ( 4, 4 ),
 ( 5.106027341939277875, 6.645403452391244414 ),
 .UNSPECIFIED. ) 
 CURVE ( )  GEOMETRIC_REPRESENTATION_ITEM ( )  RATIONAL_B_SPLINE_CURVE ( ( 1.000000000000000000, 0.8120851936182275077, 0.8120851936182275077, 1.000000000000000000 ) ) 
 REPRESENTATION_ITEM ( '' )  );
#34082=DIRECTION ( 'NONE',  ( -0.000000000000000000, 0.000000000000000000, 1.000000000000000000 ) ) ;
#34083=DIRECTION ( 'NONE',  ( -0.3543493200069162685, -0.000000000000000000, -0.9351131265310288487 ) ) ;
#34084=EDGE_CURVE ( 'NONE', #66493, #47010, #6115, .T. ) ;
#34085=CARTESIAN_POINT ( 'NONE',  ( -22.49999999999984368, -20.56887692260760048, 4.000000000000000000 ) ) ;
#34086=CARTESIAN_POINT ( 'NONE',  ( 3.328169399223507074, -6.740707523384214639, 4.000000000000000000 ) ) ;
#34087=DIRECTION ( 'NONE',  ( -0.7071067811865486830, -0.7071067811865464625, 0.000000000000000000 ) ) ;
#34090=VECTOR ( 'NONE', #24480, 1000.000000000000000 ) ;
#34092=DIRECTION ( 'NONE',  ( -0.000000000000000000, 0.000000000000000000, 1.000000000000000000 ) ) ;
#34093=FACE_OUTER_BOUND ( 'NONE', #7563, .T. ) ;
#34094=VERTEX_POINT ( 'NONE', #61314 ) ;
#34095=ORIENTED_EDGE ( 'NONE', *, *, #142052, .T. ) ;
#34097=ORIENTED_EDGE ( 'NONE', *, *, #9186, .T. ) ;
#34098=VERTEX_POINT ( 'NONE', #105452 ) ;
#34099=EDGE_CURVE ( 'NONE', #87121, #98769, #37374, .T. ) ;
#34100=VERTEX_POINT ( 'NONE', #60585 ) ;
#34102=LINE ( 'NONE', #47164, #24544 ) ;
#34103=CARTESIAN_POINT ( 'NONE',  ( 39.48921356237310221, -27.52281430457082934, 5.000000000000000000 ) ) ;
#34104=EDGE_LOOP ( 'NONE', ( #31795, #62496, #107892, #61223 ) ) ;
#34105=LINE ( 'NONE', #135558, #62514 ) ;
#34106=CARTESIAN_POINT ( 'NONE',  ( 9.707106781186476852, -9.740707523384187994, 5.000000000000000000 ) ) ;
#34107=CARTESIAN_POINT ( 'NONE',  ( -22.37177410554622980, -1.784312229707115893, 4.000000000000000000 ) ) ;
#34108=EDGE_CURVE ( 'NONE', #108030, #113572, #28651, .T. ) ;
#34109=ORIENTED_EDGE ( 'NONE', *, *, #51739, .T. ) ;
#34112=CARTESIAN_POINT ( 'NONE',  ( 34.49999999999975131, 22.21934299833216642, 4.348028800457638177 ) ) ;
#34114=DIRECTION ( 'NONE',  ( 0.7071067811865487940, 0.7071067811865463515, 0.000000000000000000 ) ) ;
#34115=CARTESIAN_POINT ( 'NONE',  ( 72.48921356237309510, -27.52281430457106026, 5.000000000000000000 ) ) ;
#34117=ORIENTED_EDGE ( 'NONE', *, *, #16711, .T. ) ;
#34122=ADVANCED_FACE ( 'NONE', ( #36363 ), #45827, .F. ) ;
#34124=DIRECTION ( 'NONE',  ( -0.7071067811865486830, -0.7071067811865464625, 0.000000000000000000 ) ) ;
#34126=LINE ( 'NONE', #121109, #78938 ) ;
#34128=ADVANCED_FACE ( 'NONE', ( #67587 ), #90758, .T. ) ;
#34129=ORIENTED_EDGE ( 'NONE', *, *, #97066, .F. ) ;
#34130=EDGE_LOOP ( 'NONE', ( #100489, #52336, #115255 ) ) ;
#34131=CARTESIAN_POINT ( 'NONE',  ( 36.65494483745359844, 5.259292476615669010, 12.77922209995902314 ) ) ;
#34132=DIRECTION ( 'NONE',  ( 1.000000000000000000, 0.000000000000000000, 0.000000000000000000 ) ) ;
#34134=ORIENTED_EDGE ( 'NONE', *, *, #3701, .F. ) ;
#34135=AXIS2_PLACEMENT_3D ( 'NONE', #28964, #62324, #60927 ) ;
#34137=EDGE_LOOP ( 'NONE', ( #97362, #12326, #124370, #70797 ) ) ;
#34138=CYLINDRICAL_SURFACE ( 'NONE', #95444, 0.5000000000000004441 ) ;
#34139=ADVANCED_FACE ( 'NONE', ( #13855 ), #124785, .T. ) ;
#34140=LINE ( 'NONE', #49130, #117299 ) ;
#34141=DIRECTION ( 'NONE',  ( -0.3543493200069162685, -0.000000000000000000, -0.9351131265310288487 ) ) ;
#34142=AXIS2_PLACEMENT_3D ( 'NONE', #91717, #100472, #35232 ) ;
#34143=VECTOR ( 'NONE', #132243, 1000.000000000000000 ) ;
#34144=AXIS2_PLACEMENT_3D ( 'NONE', #21806, #66053, #110216 ) ;
#34146=VERTEX_POINT ( 'NONE', #66848 ) ;
#34147=DIRECTION ( 'NONE',  ( 0.7071067811865487940, 0.7071067811865463515, 0.000000000000000000 ) ) ;
#34148=ORIENTED_EDGE ( 'NONE', *, *, #108715, .T. ) ;
#34149=ORIENTED_EDGE ( 'NONE', *, *, #124012, .F. ) ;
#34151=ORIENTED_EDGE ( 'NONE', *, *, #29446, .F. ) ;
#34153=DIRECTION ( 'NONE',  ( -0.6830127018922181881, 0.6830127018922202975, -0.2588190451025214056 ) ) ;
#34155=FACE_OUTER_BOUND ( 'NONE', #12538, .T. ) ;
#34156=CARTESIAN_POINT ( 'NONE',  ( -34.92500000000001137, 3.662461875838966208, 4.000000000000000000 ) ) ;
#34157=DIRECTION ( 'NONE',  ( -0.000000000000000000, 0.000000000000000000, 1.000000000000000000 ) ) ;
#34158=DIRECTION ( 'NONE',  ( 0.7071067811865487940, -0.7071067811865463515, 0.000000000000000000 ) ) ;
#34159=FACE_BOUND ( 'NONE', #139706, .T. ) ;
#34161=DIRECTION ( 'NONE',  ( -0.7071067811865486830, 0.7071067811865464625, 0.000000000000000000 ) ) ;
#34162=CARTESIAN_POINT ( 'NONE',  ( -16.63753812416086930, 22.22500000000000142, 4.000000000000000000 ) ) ;
#34163=DIRECTION ( 'NONE',  ( 0.6830127018922181881, 0.6830127018922202975, -0.2588190451025214056 ) ) ;
#34164=DIRECTION ( 'NONE',  ( -0.7071067811865487940, 0.7071067811865463515, 0.000000000000000000 ) ) ;
#34165=EDGE_LOOP ( 'NONE', ( #32941, #60812, #100450, #31151 ) ) ;
#34166=FACE_OUTER_BOUND ( 'NONE', #63677, .T. ) ;
#34167=EDGE_LOOP ( 'NONE', ( #125558, #66121, #63177, #40360 ) ) ;
#34170=ORIENTED_EDGE ( 'NONE', *, *, #20399, .F. ) ;
#34171=EDGE_CURVE ( 'NONE', #771, #123496, #12446, .T. ) ;
#34173=AXIS2_PLACEMENT_3D ( 'NONE', #17416, #37034, #105146 ) ;
#34174=VERTEX_POINT ( 'NONE', #37059 ) ;
#34175=LINE ( 'NONE', #14553, #129735 ) ;
#34176=EDGE_CURVE ( 'NONE', #110282, #140231, #111779, .T. ) ;
#34179=ADVANCED_FACE ( 'NONE', ( #56728 ), #46570, .F. ) ;
#34180=DIRECTION ( 'NONE',  ( 0.7071067811865487940, 0.7071067811865463515, 0.000000000000000000 ) ) ;
#34181=EDGE_CURVE ( 'NONE', #123762, #2143, #89310, .T. ) ;
#34182=CARTESIAN_POINT ( 'NONE',  ( -18.48921356237309510, -27.52281430457068367, 5.000000000000000000 ) ) ;
#34183=DIRECTION ( 'NONE',  ( -0.7071067811865486830, -0.7071067811865464625, 0.000000000000000000 ) ) ;
#34184=DIRECTION ( 'NONE',  ( 0.000000000000000000, 0.000000000000000000, 1.000000000000000000 ) ) ;
#34185=PLANE ( 'NONE',  #10060 ) ;
#34186=ORIENTED_EDGE ( 'NONE', *, *, #63618, .T. ) ;
#34187=VERTEX_POINT ( 'NONE', #90002 ) ;
#34188=EDGE_LOOP ( 'NONE', ( #101326, #74284, #46371, #97469 ) ) ;
#34190=DIRECTION ( 'NONE',  ( 0.6830127018922181881, 0.6830127018922202975, -0.2588190451025214056 ) ) ;
#34191=CARTESIAN_POINT ( 'NONE',  ( -54.48921356237310221, -27.52281430457093236, 5.000000000000000000 ) ) ;
#34192=EDGE_LOOP ( 'NONE', ( #43865, #84618, #17716, #45897 ) ) ;
#34193=ORIENTED_EDGE ( 'NONE', *, *, #25541, .F. ) ;
#34195=DIRECTION ( 'NONE',  ( 0.7071067811865487940, 0.7071067811865463515, 0.000000000000000000 ) ) ;
#34196=EDGE_CURVE ( 'NONE', #120984, #27268, #55996, .T. ) ;
#34198=LINE ( 'NONE', #34920, #138951 ) ;
#34199=ORIENTED_EDGE ( 'NONE', *, *, #74245, .F. ) ;
#34200=CARTESIAN_POINT ( 'NONE',  ( -63.29974487139158867, -27.71228299555250274, 4.000000000000000000 ) ) ;
#34201=EDGE_CURVE ( 'NONE', #114640, #15762, #24758, .T. ) ;
#34202=CARTESIAN_POINT ( 'NONE',  ( -34.92500000000001137, -2.038703271653886429, -4.194424194487899271 ) ) ;
#34204=DIRECTION ( 'NONE',  ( -0.6830127018922180770, -0.6830127018922204085, -0.2588190451025213501 ) ) ;
#34205=ORIENTED_EDGE ( 'NONE', *, *, #10281, .F. ) ;
#34208=DIRECTION ( 'NONE',  ( 0.7071067811865487940, 0.7071067811865463515, -0.000000000000000000 ) ) ;
#34210=CARTESIAN_POINT ( 'NONE',  ( 1.171830600776465392, -5.240707523384232402, 4.000000000000000000 ) ) ;
#34211=EDGE_CURVE ( 'NONE', #74950, #4967, #78439, .T. ) ;
#34212=CARTESIAN_POINT ( 'NONE',  ( 0.000000000000000000, -21.72500000000000142, 4.500000000000000888 ) ) ;
#34213=VERTEX_POINT ( 'NONE', #113180 ) ;
#34214=CARTESIAN_POINT ( 'NONE',  ( -42.48921356237308800, -27.52281430457085065, 5.000000000000000000 ) ) ;
#34215=ORIENTED_EDGE ( 'NONE', *, *, #93924, .T. ) ;
#34217=FACE_OUTER_BOUND ( 'NONE', #132297, .T. ) ;
#34218=LINE ( 'NONE', #79906, #75025 ) ;
#34219=VERTEX_POINT ( 'NONE', #102348 ) ;
#34221=FACE_OUTER_BOUND ( 'NONE', #88914, .T. ) ;
#34223=VERTEX_POINT ( 'NONE', #94987 ) ;
#34224=AXIS2_PLACEMENT_3D ( 'NONE', #45999, #77205, #90928 ) ;
#34225=CARTESIAN_POINT ( 'NONE',  ( -3.707106781186516375, 8.259292476615639700, 5.000000000000000000 ) ) ;
#34226=VERTEX_POINT ( 'NONE', #73284 ) ;
#34227=VECTOR ( 'NONE', #31651, 1000.000000000000000 ) ;
#34228=DIRECTION ( 'NONE',  ( -0.7071067811865487940, 0.7071067811865463515, 0.000000000000000000 ) ) ;
#34231=VERTEX_POINT ( 'NONE', #5827 ) ;
#34233=CARTESIAN_POINT ( 'NONE',  ( -2.999999999999971578, -19.44781430457064175, 5.000000000000000000 ) ) ;
#34234=VECTOR ( 'NONE', #135457, 1000.000000000000000 ) ;
#34236=VECTOR ( 'NONE', #58091, 1000.000000000000227 ) ;
#34237=EDGE_CURVE ( 'NONE', #100336, #69474, #49409, .T. ) ;
#34238=LINE ( 'NONE', #78460, #25121 ) ;
#34239=DIRECTION ( 'NONE',  ( -0.7071067811865486830, -0.7071067811865464625, 0.000000000000000000 ) ) ;
#34240=CARTESIAN_POINT ( 'NONE',  ( 19.05000000000000071, 3.174999999999997158, 4.000000000000000000 ) ) ;
#34241=VERTEX_POINT ( 'NONE', #15273 ) ;
#34242=LINE ( 'NONE', #1565, #90550 ) ;
#34243=EDGE_CURVE ( 'NONE', #65901, #99074, #72604, .T. ) ;
#34244=CARTESIAN_POINT ( 'NONE',  ( -2.994519915287485734, 28.92564299267940342, 4.000000000000000000 ) ) ;
#34245=PLANE ( 'NONE',  #67894 ) ;
#34246=DIRECTION ( 'NONE',  ( -0.000000000000000000, -0.3543493200069152693, 0.9351131265310292928 ) ) ;
#34249=EDGE_LOOP ( 'NONE', ( #1863, #28587, #67206, #138658 ) ) ;
#34250=ORIENTED_EDGE ( 'NONE', *, *, #93760, .F. ) ;
#34251=ORIENTED_EDGE ( 'NONE', *, *, #30080, .F. ) ;
#34253=EDGE_CURVE ( 'NONE', #14203, #45336, #26900, .T. ) ;
#34254=VERTEX_POINT ( 'NONE', #37804 ) ;
#34256=CARTESIAN_POINT ( 'NONE',  ( -24.48921356237309510, -27.52281430457072631, 5.000000000000000000 ) ) ;
#34257=ORIENTED_EDGE ( 'NONE', *, *, #119030, .T. ) ;
#34258=DIRECTION ( 'NONE',  ( 0.7071067811865486830, -0.7071067811865464625, -0.000000000000000000 ) ) ;
#34259=DIRECTION ( 'NONE',  ( 1.000000000000000000, 0.000000000000000000, 0.000000000000000000 ) ) ;
#34260=LINE ( 'NONE', #45172, #41717 ) ;
#34261=DIRECTION ( 'NONE',  ( 0.7071067811865487940, -0.7071067811865463515, 0.000000000000000000 ) ) ;
#34263=EDGE_CURVE ( 'NONE', #50240, #142853, #82039, .T. ) ;
#34264=ORIENTED_EDGE ( 'NONE', *, *, #90339, .F. ) ;
#34266=CARTESIAN_POINT ( 'NONE',  ( -8.671830600776408104, -18.74070752338409562, 4.000000000000000000 ) ) ;
#34268=LINE ( 'NONE', #67643, #20231 ) ;
#34269=CARTESIAN_POINT ( 'NONE',  ( -57.48921356237308800, -27.52281430457095368, 5.000000000000000000 ) ) ;
#34270=DIRECTION ( 'NONE',  ( -0.7071067811865486830, 0.7071067811865464625, 0.000000000000000000 ) ) ;
#34273=LINE ( 'NONE', #122691, #7407 ) ;
#34274=CARTESIAN_POINT ( 'NONE',  ( 14.20710678118644665, -5.240707523384228850, 5.000000000000000000 ) ) ;
#34278=CARTESIAN_POINT ( 'NONE',  ( -18.48921356237309510, -27.52281430457068367, 5.000000000000000000 ) ) ;
#34279=EDGE_CURVE ( 'NONE', #2943, #82308, #117452, .T. ) ;
#34280=LINE ( 'NONE', #119822, #120186 ) ;
#34281=EDGE_LOOP ( 'NONE', ( #135909, #30837, #129870, #97019 ) ) ;
#34282=DIRECTION ( 'NONE',  ( 0.7071067811865486830, 0.7071067811865463515, 0.000000000000000000 ) ) ;
#34283=LINE ( 'NONE', #78504, #74682 ) ;
#34285=EDGE_CURVE ( 'NONE', #4808, #5121, #59559, .T. ) ;
#34287=ORIENTED_EDGE ( 'NONE', *, *, #117351, .F. ) ;
#34288=ORIENTED_EDGE ( 'NONE', *, *, #1120, .T. ) ;
#34289=CARTESIAN_POINT ( 'NONE',  ( -54.18398860626899705, 28.73617430169825226, 5.000000000000000000 ) ) ;
#34290=CARTESIAN_POINT ( 'NONE',  ( 0.5752130600809799432, 22.22500000000000142, -8.452357796116274358 ) ) ;
#34291=FACE_OUTER_BOUND ( 'NONE', #37635, .T. ) ;
#34292=LINE ( 'NONE', #100965, #92580 ) ;
#34293=ORIENTED_EDGE ( 'NONE', *, *, #7309, .T. ) ;
#34294=EDGE_CURVE ( 'NONE', #109431, #28308, #17443, .T. ) ;
#34295=CARTESIAN_POINT ( 'NONE',  ( -45.18398860626900415, 28.73617430169818832, 5.000000000000000000 ) ) ;
#34296=VERTEX_POINT ( 'NONE', #138527 ) ;
#34299=CARTESIAN_POINT ( 'NONE',  ( 41.99451991528749062, 28.92564299267967343, 4.000000000000000000 ) ) ;
#34300=DIRECTION ( 'NONE',  ( -0.7071067811865486830, -0.7071067811865464625, -0.000000000000000000 ) ) ;
#34302=DIRECTION ( 'NONE',  ( -0.7071067811865486830, 0.7071067811865464625, 0.000000000000000000 ) ) ;
#34303=CARTESIAN_POINT ( 'NONE',  ( -9.299744871391588674, -27.71228299555212971, 4.000000000000000000 ) ) ;
#34304=ORIENTED_EDGE ( 'NONE', *, *, #81017, .T. ) ;
#34305=AXIS2_PLACEMENT_3D ( 'NONE', #86606, #41644, #51834 ) ;
#34306=PLANE ( 'NONE',  #138010 ) ;
#34308=CARTESIAN_POINT ( 'NONE',  ( -72.48921356237309510, -27.52281430457106026, 5.000000000000000000 ) ) ;
#34309=LINE ( 'NONE', #65552, #6044 ) ;
#34310=DIRECTION ( 'NONE',  ( 0.7071067811865487940, -0.7071067811865463515, 0.000000000000000000 ) ) ;
#34311=ORIENTED_EDGE ( 'NONE', *, *, #111158, .F. ) ;
#34314=EDGE_CURVE ( 'NONE', #37230, #49472, #116760, .T. ) ;
#34315=ADVANCED_BREP_SHAPE_REPRESENTATION ( '', ( #45918, #127880 ), #137188 ) ;
#34316=CARTESIAN_POINT ( 'NONE',  ( -26.99999999999981171, -16.06887692260764666, 4.000000000000000000 ) ) ;
#34317=ORIENTED_EDGE ( 'NONE', *, *, #41753, .F. ) ;
#34318=CARTESIAN_POINT ( 'NONE',  ( -35.99451991528749772, 28.92564299267963079, 4.000000000000000000 ) ) ;
#34319=LINE ( 'NONE', #111135, #20132 ) ;
#34320=CARTESIAN_POINT ( 'NONE',  ( 18.48921356237309510, -27.52281430457068367, 5.000000000000000000 ) ) ;
#34322=CARTESIAN_POINT ( 'NONE',  ( -23.99999999999983302, -18.03360074219755660, 5.000000000000000000 ) ) ;
#34324=FACE_BOUND ( 'NONE', #75392, .T. ) ;
#34325=DIRECTION ( 'NONE',  ( 0.7071067811865487940, -0.7071067811865463515, 0.000000000000000000 ) ) ;
#34326=DIRECTION ( 'NONE',  ( -0.000000000000000000, -0.3543493200069152693, 0.9351131265310292928 ) ) ;
#34327=EDGE_CURVE ( 'NONE', #58810, #94676, #137824, .T. ) ;
#34328=CARTESIAN_POINT ( 'NONE',  ( 14.99999999999989164, -21.41253812416053748, 4.000000000000000000 ) ) ;
#34330=EDGE_LOOP ( 'NONE', ( #3169, #66886, #126298, #84762 ) ) ;
#34332=VECTOR ( 'NONE', #25238, 1000.000000000000000 ) ;
#34333=DIRECTION ( 'NONE',  ( -0.7071067811865486830, 0.7071067811865464625, 0.000000000000000000 ) ) ;
#34334=ORIENTED_EDGE ( 'NONE', *, *, #106642, .F. ) ;
#34335=EDGE_CURVE ( 'NONE', #89571, #41615, #26199, .T. ) ;
#34336=ORIENTED_EDGE ( 'NONE', *, *, #139627, .F. ) ;
#34338=ORIENTED_EDGE ( 'NONE', *, *, #89021, .F. ) ;
#34339=FACE_OUTER_BOUND ( 'NONE', #26228, .T. ) ;
#34340=EDGE_CURVE ( 'NONE', #112149, #89022, #15982, .T. ) ;
#34341=ORIENTED_EDGE ( 'NONE', *, *, #135193, .F. ) ;
#34342=PLANE ( 'NONE',  #19247 ) ;
#34343=VECTOR ( 'NONE', #46589, 1000.000000000000000 ) ;
#34344=EDGE_CURVE ( 'NONE', #96477, #127633, #128373, .T. ) ;
#34345=EDGE_CURVE ( 'NONE', #100536, #96477, #29045, .T. ) ;
#34346=PLANE ( 'NONE',  #5555 ) ;
#34348=DIRECTION ( 'NONE',  ( 0.7071067811865487940, 0.7071067811865463515, 0.000000000000000000 ) ) ;
#34350=CARTESIAN_POINT ( 'NONE',  ( -65.99451991528749772, 28.92564299267984396, 4.000000000000000000 ) ) ;
#34351=CARTESIAN_POINT ( 'NONE',  ( -50.99451991528749062, 28.92564299267973738, 4.000000000000000000 ) ) ;
#34353=PLANE ( 'NONE',  #55547 ) ;
#34354=ORIENTED_EDGE ( 'NONE', *, *, #32833, .T. ) ;
#34355=VECTOR ( 'NONE', #56934, 999.9999999999998863 ) ;
#34356=ORIENTED_EDGE ( 'NONE', *, *, #127480, .T. ) ;
#34357=CARTESIAN_POINT ( 'NONE',  ( -28.49999999999980105, -10.04351517176480613, -1.623559851933888964 ) ) ;
#34358=( BOUNDED_CURVE ( )  B_SPLINE_CURVE ( 3, ( #136275, #16629, #125420, #72502 ),
 .UNSPECIFIED., .F., .T. ) 
 B_SPLINE_CURVE_WITH_KNOTS ( ( 4, 4 ),
 ( 5.005968288816732503, 5.074607125596331869 ),
 .UNSPECIFIED. ) 
 CURVE ( )  GEOMETRIC_REPRESENTATION_ITEM ( )  RATIONAL_B_SPLINE_CURVE ( ( 1.000000000000000000, 0.9996074310407765395, 0.9996074310407765395, 1.000000000000000000 ) ) 
 REPRESENTATION_ITEM ( '' )  );
#34359=CARTESIAN_POINT ( 'NONE',  ( 69.29974487139159578, -27.71228299555254537, 4.000000000000000000 ) ) ;
#34360=EDGE_LOOP ( 'NONE', ( #41169, #74798, #78924, #42805 ) ) ;
#34362=VECTOR ( 'NONE', #100697, 999.9999999999998863 ) ;
#34364=ADVANCED_FACE ( 'NONE', ( #4362 ), #48665, .F. ) ;
#34365=ADVANCED_FACE ( 'NONE', ( #116034 ), #16736, .F. ) ;
#34366=LINE ( 'NONE', #79344, #99367 ) ;
#34367=EDGE_LOOP ( 'NONE', ( #52874, #139272, #74067, #54223 ) ) ;
#34368=LINE ( 'NONE', #78588, #127298 ) ;
#34369=EDGE_CURVE ( 'NONE', #142313, #134912, #108703, .T. ) ;
#34370=CARTESIAN_POINT ( 'NONE',  ( -42.48921356237308800, -27.52281430457085065, 5.000000000000000000 ) ) ;
#34375=DIRECTION ( 'NONE',  ( -0.7071067811865487940, 0.7071067811865463515, -0.000000000000000000 ) ) ;
#34377=AXIS2_PLACEMENT_3D ( 'NONE', #129016, #73934, #118111 ) ;
#34380=VERTEX_POINT ( 'NONE', #141370 ) ;
#34381=CARTESIAN_POINT ( 'NONE',  ( 1.499999999999990896, 6.277155672890271099, -3.510561720658945450 ) ) ;
#34383=CARTESIAN_POINT ( 'NONE',  ( 3.654944837453800943, 5.259292476615669010, 12.77922209995894498 ) ) ;
#34384=ORIENTED_EDGE ( 'NONE', *, *, #94714, .F. ) ;
#34385=CARTESIAN_POINT ( 'NONE',  ( -5.999999999999960032, 5.587461875839188075, 4.000000000000000000 ) ) ;
#34386=ORIENTED_EDGE ( 'NONE', *, *, #76083, .F. ) ;
#34389=LINE ( 'NONE', #88789, #84276 ) ;
#34390=ADVANCED_FACE ( 'NONE', ( #19588 ), #7981, .F. ) ;
#34392=LINE ( 'NONE', #14774, #70194 ) ;
#34393=PLANE ( 'NONE',  #88535 ) ;
#34394=DIRECTION ( 'NONE',  ( 0.3543493200069162685, -0.000000000000000000, -0.9351131265310288487 ) ) ;
#34395=LINE ( 'NONE', #2446, #92299 ) ;
#34396=ORIENTED_EDGE ( 'NONE', *, *, #61374, .F. ) ;
#34397=EDGE_CURVE ( 'NONE', #123427, #36268, #87706, .T. ) ;
#34398=ORIENTED_EDGE ( 'NONE', *, *, #33067, .F. ) ;
#34399=ADVANCED_FACE ( 'NONE', ( #63132 ), #130520, .F. ) ;
#34400=CARTESIAN_POINT ( 'NONE',  ( 57.18398860626899705, 28.73617430169827358, 5.000000000000000000 ) ) ;
#34401=DIRECTION ( 'NONE',  ( 0.7071067811865486830, -0.7071067811865464625, -0.000000000000000000 ) ) ;
#34402=EDGE_CURVE ( 'NONE', #46120, #51714, #10828, .T. ) ;
#34405=ORIENTED_EDGE ( 'NONE', *, *, #58246, .T. ) ;
#34406=DIRECTION ( 'NONE',  ( -0.6830127018922181881, 0.6830127018922202975, -0.2588190451025214056 ) ) ;
#34407=FACE_OUTER_BOUND ( 'NONE', #143328, .T. ) ;
#34409=LINE ( 'NONE', #69192, #113607 ) ;
#34410=CARTESIAN_POINT ( 'NONE',  ( 7.213219033033542615, 12.75929247661559351, 10.29404684609036913 ) ) ;
#34411=CARTESIAN_POINT ( 'NONE',  ( 11.99999999999991651, 7.588810512006220144, -3.013526669885254972 ) ) ;
#34412=CARTESIAN_POINT ( 'NONE',  ( -15.18398860626900237, 28.73617430169797871, 5.000000000000000000 ) ) ;
#34414=LINE ( 'NONE', #44625, #113601 ) ;
#34415=LINE ( 'NONE', #43877, #60368 ) ;
#34416=VECTOR ( 'NONE', #51528, 999.9999999999998863 ) ;
#34417=DIRECTION ( 'NONE',  ( 0.3543493200069162685, -0.000000000000000000, -0.9351131265310288487 ) ) ;
#34418=ORIENTED_EDGE ( 'NONE', *, *, #59614, .F. ) ;
#34419=CARTESIAN_POINT ( 'NONE',  ( 20.99451991528748707, 28.92564299267952777, 4.000000000000000000 ) ) ;
#34420=ORIENTED_EDGE ( 'NONE', *, *, #104569, .T. ) ;
#34421=CARTESIAN_POINT ( 'NONE',  ( -48.48921356237309510, -27.52281430457089328, 5.000000000000000000 ) ) ;
#34423=VECTOR ( 'NONE', #85922, 1000.000000000000227 ) ;
#34425=FACE_OUTER_BOUND ( 'NONE', #1623, .T. ) ;
#34426=CARTESIAN_POINT ( 'NONE',  ( 1.499999999999996225, -10.91253812416064406, 4.000000000000000000 ) ) ;
#34427=VECTOR ( 'NONE', #31303, 1000.000000000000000 ) ;
#34428=DIRECTION ( 'NONE',  ( 1.000000000000000000, 0.000000000000000000, 0.000000000000000000 ) ) ;
#34429=PLANE ( 'NONE',  #12977 ) ;
#34430=ORIENTED_EDGE ( 'NONE', *, *, #43746, .F. ) ;
#34431=EDGE_LOOP ( 'NONE', ( #44970, #81356, #51541, #61162 ) ) ;
#34432=CARTESIAN_POINT ( 'NONE',  ( -27.31657961132772883, -6.740707523384216415, 11.88629033278130542 ) ) ;
#34435=VECTOR ( 'NONE', #10955, 1000.000000000000000 ) ;
#34436=VECTOR ( 'NONE', #27852, 999.9999999999998863 ) ;
#34437=LINE ( 'NONE', #66367, #1074 ) ;
#34440=CARTESIAN_POINT ( 'NONE',  ( -34.75611968250420603, -10.29434930147582783, 4.955485411084898040 ) ) ;
#34441=DIRECTION ( 'NONE',  ( 0.7071067811865487940, 0.7071067811865463515, -0.000000000000000000 ) ) ;
#34442=ORIENTED_EDGE ( 'NONE', *, *, #23993, .F. ) ;
#34444=DIRECTION ( 'NONE',  ( 0.6830127018922180770, -0.6830127018922204085, -0.2588190451025214056 ) ) ;
#34445=DIRECTION ( 'NONE',  ( -0.7071067811865486830, -0.7071067811865464625, 0.000000000000000000 ) ) ;
#34446=CARTESIAN_POINT ( 'NONE',  ( 24.18398860626899705, 28.73617430169804265, 5.000000000000000000 ) ) ;
#34447=VECTOR ( 'NONE', #124628, 1000.000000000000000 ) ;
#34448=VECTOR ( 'NONE', #108222, 1000.000000000000000 ) ;
#34449=ORIENTED_EDGE ( 'NONE', *, *, #142516, .F. ) ;
#34450=DIRECTION ( 'NONE',  ( 0.3543493200069162685, -0.000000000000000000, -0.9351131265310288487 ) ) ;
#34452=CARTESIAN_POINT ( 'NONE',  ( 0.000000000000000000, 0.000000000000000000, 5.000000000000000000 ) ) ;
#34454=AXIS2_PLACEMENT_3D ( 'NONE', #140001, #5859, #60301 ) ;
#34455=ORIENTED_EDGE ( 'NONE', *, *, #97849, .F. ) ;
#34456=ORIENTED_EDGE ( 'NONE', *, *, #106436, .T. ) ;
#34457=AXIS2_PLACEMENT_3D ( 'NONE', #66908, #111088, #11780 ) ;
#34458=CARTESIAN_POINT ( 'NONE',  ( 32.99999999999977973, 2.587461875839218273, 4.000000000000000000 ) ) ;
#34459=VECTOR ( 'NONE', #100210, 1000.000000000000227 ) ;
#34460=DIRECTION ( 'NONE',  ( 0.6830127018922181881, 0.6830127018922202975, -0.2588190451025214056 ) ) ;
#34461=CARTESIAN_POINT ( 'NONE',  ( 14.99999999999990585, -16.44781430457066662, 5.000000000000000000 ) ) ;
#34462=VECTOR ( 'NONE', #39606, 1000.000000000000227 ) ;
#34463=DIRECTION ( 'NONE',  ( 0.3543493200069162685, -0.000000000000000000, -0.9351131265310288487 ) ) ;
#34465=CARTESIAN_POINT ( 'NONE',  ( -14.54016161050250844, 18.75929247661552779, 8.305906642995452671 ) ) ;
#34466=DIRECTION ( 'NONE',  ( -0.000000000000000000, -0.3543493200069152693, 0.9351131265310292928 ) ) ;
#34467=ORIENTED_EDGE ( 'NONE', *, *, #135902, .F. ) ;
#34468=EDGE_CURVE ( 'NONE', #87036, #52226, #55090, .T. ) ;
#34470=LINE ( 'NONE', #24303, #82368 ) ;
#34472=VECTOR ( 'NONE', #106411, 999.9999999999998863 ) ;
#34473=DIRECTION ( 'NONE',  ( 0.6830127018922181881, 0.6830127018922202975, -0.2588190451025214056 ) ) ;
#34474=AXIS2_PLACEMENT_3D ( 'NONE', #91773, #112124, #34554 ) ;
#34475=ORIENTED_EDGE ( 'NONE', *, *, #64775, .T. ) ;
#34479=EDGE_CURVE ( 'NONE', #106022, #124937, #97874, .T. ) ;
#34480=DIRECTION ( 'NONE',  ( -0.6830127018922181881, 0.6830127018922202975, -0.2588190451025214056 ) ) ;
#34481=CARTESIAN_POINT ( 'NONE',  ( 27.78162688292474769, 21.74787736706806740, 4.999607392498048419 ) ) ;
#34482=CARTESIAN_POINT ( 'NONE',  ( 1.828169399223519953, -11.24070752338416845, 4.000000000000000000 ) ) ;
#34484=ORIENTED_EDGE ( 'NONE', *, *, #60923, .T. ) ;
#34485=ORIENTED_EDGE ( 'NONE', *, *, #22718, .F. ) ;
#34486=VECTOR ( 'NONE', #12627, 999.9999999999998863 ) ;
#34489=EDGE_CURVE ( 'NONE', #6107, #38956, #52219, .T. ) ;
#34490=ORIENTED_EDGE ( 'NONE', *, *, #105076, .T. ) ;
#34491=CARTESIAN_POINT ( 'NONE',  ( 30.79289321881325137, -20.24070752338407431, 5.000000000000000000 ) ) ;
#34492=FACE_OUTER_BOUND ( 'NONE', #132695, .T. ) ;
#34493=PLANE ( 'NONE',  #65566 ) ;
#34494=ADVANCED_FACE ( 'NONE', ( #54400 ), #52902, .T. ) ;
#34495=EDGE_LOOP ( 'NONE', ( #22923, #114917, #25166, #8951 ) ) ;
#34496=FACE_BOUND ( 'NONE', #46536, .T. ) ;
#34497=DIRECTION ( 'NONE',  ( 0.7071067811865487940, 0.7071067811865463515, 0.000000000000000000 ) ) ;
#34498=PLANE ( 'NONE',  #86040 ) ;
#34499=CARTESIAN_POINT ( 'NONE',  ( 14.51078643762690490, -27.52281430457045275, 5.000000000000000000 ) ) ;
#34501=FACE_OUTER_BOUND ( 'NONE', #105829, .T. ) ;
#34504=ORIENTED_EDGE ( 'NONE', *, *, #141234, .F. ) ;
#34506=ORIENTED_EDGE ( 'NONE', *, *, #33758, .T. ) ;
#34507=ORIENTED_EDGE ( 'NONE', *, *, #42046, .F. ) ;
#34508=EDGE_CURVE ( 'NONE', #9125, #40590, #119591, .T. ) ;
#34509=CARTESIAN_POINT ( 'NONE',  ( -14.99451991528749595, 28.92564299267948513, 4.000000000000000000 ) ) ;
#34511=EDGE_CURVE ( 'NONE', #4615, #48007, #65992, .T. ) ;
#34513=LINE ( 'NONE', #122955, #84156 ) ;
#34514=VERTEX_POINT ( 'NONE', #118159 ) ;
#34515=CARTESIAN_POINT ( 'NONE',  ( -6.328169399223487090, 14.25929247661557575, 4.000000000000000000 ) ) ;
#34516=DIRECTION ( 'NONE',  ( 0.6830127018922181881, 0.6830127018922202975, -0.2588190451025214056 ) ) ;
#34517=DIRECTION ( 'NONE',  ( -0.7071067811865486830, 0.7071067811865464625, 0.000000000000000000 ) ) ;
#34519=CARTESIAN_POINT ( 'NONE',  ( -39.18398860626899705, 28.73617430169814568, 5.000000000000000000 ) ) ;
#34520=DIRECTION ( 'NONE',  ( 0.000000000000000000, 1.000000000000000000, -0.000000000000000000 ) ) ;
#34521=VECTOR ( 'NONE', #138624, 1000.000000000000227 ) ;
#34522=VECTOR ( 'NONE', #18429, 1000.000000000000227 ) ;
#34524=CARTESIAN_POINT ( 'NONE',  ( 0.000000000000000000, 0.000000000000000000, 5.000000000000000000 ) ) ;
#34525=ORIENTED_EDGE ( 'NONE', *, *, #132716, .T. ) ;
#34526=EDGE_CURVE ( 'NONE', #45818, #34226, #109456, .T. ) ;
#34528=DIRECTION ( 'NONE',  ( 1.000000000000000000, 0.000000000000000000, 0.000000000000000000 ) ) ;
#34529=AXIS2_PLACEMENT_3D ( 'NONE', #129701, #30409, #130452 ) ;
#34530=ORIENTED_EDGE ( 'NONE', *, *, #122834, .T. ) ;
#34531=EDGE_LOOP ( 'NONE', ( #22615, #6234, #63044, #3037 ) ) ;
#34532=EDGE_CURVE ( 'NONE', #128563, #28263, #99261, .T. ) ;
#34533=ADVANCED_FACE ( 'NONE', ( #29734 ), #73981, .F. ) ;
#34536=VERTEX_POINT ( 'NONE', #68838 ) ;
#34537=VECTOR ( 'NONE', #87729, 1000.000000000000227 ) ;
#34539=CARTESIAN_POINT ( 'NONE',  ( 11.20710678118647508, 0.7592924766157104211, 5.000000000000000000 ) ) ;
#34540=( BOUNDED_CURVE ( )  B_SPLINE_CURVE ( 3, ( #26892, #60266, #17437, #129772 ),
 .UNSPECIFIED., .F., .F. ) 
 B_SPLINE_CURVE_WITH_KNOTS ( ( 4, 4 ),
 ( 1.901594255663625388, 1.933014472006574280 ),
 .UNSPECIFIED. ) 
 CURVE ( )  GEOMETRIC_REPRESENTATION_ITEM ( )  RATIONAL_B_SPLINE_CURVE ( ( 1.000000000000000000, 0.9999177325257868620, 0.9999177325257868620, 1.000000000000000000 ) ) 
 REPRESENTATION_ITEM ( '' )  );
#34543=LINE ( 'NONE', #135987, #116548 ) ;
#34544=EDGE_CURVE ( 'NONE', #1349, #105081, #121740, .T. ) ;
#34545=ORIENTED_EDGE ( 'NONE', *, *, #28598, .T. ) ;
#34546=ORIENTED_EDGE ( 'NONE', *, *, #79102, .T. ) ;
#34547=PLANE ( 'NONE',  #46472 ) ;
#34548=VECTOR ( 'NONE', #60851, 1000.000000000000227 ) ;
#34549=AXIS2_PLACEMENT_3D ( 'NONE', #11782, #131457, #43028 ) ;
#34550=EDGE_CURVE ( 'NONE', #113756, #80227, #123909, .T. ) ;
#34551=CARTESIAN_POINT ( 'NONE',  ( -60.18398860626900415, 28.73617430169829490, 5.000000000000000000 ) ) ;
#34553=LINE ( 'NONE', #67939, #141840 ) ;
#34554=DIRECTION ( 'NONE',  ( -0.7071067811865486830, 0.7071067811865464625, 0.000000000000000000 ) ) ;
#34555=LINE ( 'NONE', #43293, #42863 ) ;
#34556=VERTEX_POINT ( 'NONE', #79743 ) ;
#34557=VECTOR ( 'NONE', #129279, 1000.000000000000000 ) ;
#34558=CARTESIAN_POINT ( 'NONE',  ( 18.98911971346037930, -22.02621442084248216, 4.990779571109221102 ) ) ;
#34559=ORIENTED_EDGE ( 'NONE', *, *, #94726, .F. ) ;
#34560=ORIENTED_EDGE ( 'NONE', *, *, #118806, .T. ) ;
#34561=ORIENTED_EDGE ( 'NONE', *, *, #75173, .T. ) ;
#34562=CARTESIAN_POINT ( 'NONE',  ( 39.48921356237310221, -27.52281430457082934, 5.000000000000000000 ) ) ;
#34563=VECTOR ( 'NONE', #23583, 999.9999999999998863 ) ;
#34564=VECTOR ( 'NONE', #98948, 1000.000000000000000 ) ;
#34565=DIRECTION ( 'NONE',  ( 0.7071067811865487940, 0.7071067811865463515, 0.000000000000000000 ) ) ;
#34568=CARTESIAN_POINT ( 'NONE',  ( 6.299744871391586898, -27.71228299555210484, 4.000000000000000000 ) ) ;
#34569=CARTESIAN_POINT ( 'NONE',  ( 13.00193056682088688, -22.22500000000000142, 4.500000000000000888 ) ) ;
#34570=ORIENTED_EDGE ( 'NONE', *, *, #73842, .T. ) ;
#34571=VECTOR ( 'NONE', #105554, 1000.000000000000000 ) ;
#34572=LINE ( 'NONE', #123009, #74845 ) ;
#34573=EDGE_CURVE ( 'NONE', #104604, #23136, #34766, .T. ) ;
#34574=EDGE_CURVE ( 'NONE', #99644, #119678, #36195, .T. ) ;
#34576=LINE ( 'NONE', #35314, #74059 ) ;
#34577=CARTESIAN_POINT ( 'NONE',  ( 29.99999999999978328, 17.58746187583907172, 4.000000000000000000 ) ) ;
#34578=CARTESIAN_POINT ( 'NONE',  ( -0.1839886062690032631, 28.73617430169787568, 5.000000000000000000 ) ) ;
#34579=ORIENTED_EDGE ( 'NONE', *, *, #100328, .F. ) ;
#34580=ORIENTED_EDGE ( 'NONE', *, *, #14780, .T. ) ;
#34581=VERTEX_POINT ( 'NONE', #46389 ) ;
#34582=DIRECTION ( 'NONE',  ( -0.6830127018922181881, 0.6830127018922202975, -0.2588190451025214056 ) ) ;
#34584=VECTOR ( 'NONE', #48855, 999.9999999999998863 ) ;
#34585=DIRECTION ( 'NONE',  ( 0.6830127018922181881, 0.6830127018922202975, -0.2588190451025214056 ) ) ;
#34586=CARTESIAN_POINT ( 'NONE',  ( 27.29974487139158512, -27.71228299555225405, 4.000000000000000000 ) ) ;
#34590=FACE_OUTER_BOUND ( 'NONE', #6797, .T. ) ;
#34591=FACE_OUTER_BOUND ( 'NONE', #29160, .T. ) ;
#34592=EDGE_LOOP ( 'NONE', ( #30785, #109275, #45922, #78497 ) ) ;
#34593=PLANE ( 'NONE',  #129850 ) ;
#34594=ORIENTED_EDGE ( 'NONE', *, *, #141859, .F. ) ;
#34598=CARTESIAN_POINT ( 'NONE',  ( 2.475998614145494603, 22.03583458319438648, 4.979811245910084061 ) ) ;
#34599=VERTEX_POINT ( 'NONE', #2824 ) ;
#34600=CARTESIAN_POINT ( 'NONE',  ( -26.99451991528749417, 28.92564299267956685, 4.000000000000000000 ) ) ;
#34602=ORIENTED_EDGE ( 'NONE', *, *, #103559, .T. ) ;
#34603=CARTESIAN_POINT ( 'NONE',  ( 15.48921356237309510, -27.52281430457066236, 5.000000000000000000 ) ) ;
#34605=PLANE ( 'NONE',  #69954 ) ;
#34606=VERTEX_POINT ( 'NONE', #134812 ) ;
#34610=CARTESIAN_POINT ( 'NONE',  ( 19.21071296386495675, 9.141836041257182188, 4.000000000000000000 ) ) ;
#34611=ORIENTED_EDGE ( 'NONE', *, *, #80918, .T. ) ;
#34612=CARTESIAN_POINT ( 'NONE',  ( 32.99451991528749062, 28.92564299267960948, 4.000000000000000000 ) ) ;
#34613=EDGE_CURVE ( 'NONE', #25257, #21326, #133370, .T. ) ;
#34614=LINE ( 'NONE', #13541, #106248 ) ;
#34617=DIRECTION ( 'NONE',  ( -0.7071067811865486830, -0.7071067811865464625, 0.000000000000000000 ) ) ;
#34619=ORIENTED_EDGE ( 'NONE', *, *, #52294, .F. ) ;
#34620=ORIENTED_EDGE ( 'NONE', *, *, #104940, .T. ) ;
#34621=CARTESIAN_POINT ( 'NONE',  ( 11.99999999999991296, -10.06887692260771239, 4.000000000000000000 ) ) ;
#34622=ORIENTED_EDGE ( 'NONE', *, *, #102664, .F. ) ;
#34623=VECTOR ( 'NONE', #21742, 1000.000000000000000 ) ;
#34625=PLANE ( 'NONE',  #112616 ) ;
#34626=CARTESIAN_POINT ( 'NONE',  ( -34.42500000000001137, 0.000000000000000000, 4.500000000000000888 ) ) ;
#34627=VECTOR ( 'NONE', #60753, 1000.000000000000000 ) ;
#34628=CARTESIAN_POINT ( 'NONE',  ( 33.48921356237309510, -27.52281430457078670, 5.000000000000000000 ) ) ;
#34629=CARTESIAN_POINT ( 'NONE',  ( -18.29974487139159223, -27.71228299555219010, 4.000000000000000000 ) ) ;
#34630=ORIENTED_EDGE ( 'NONE', *, *, #139243, .T. ) ;
#34631=AXIS2_PLACEMENT_3D ( 'NONE', #7205, #118109, #139927 ) ;
#34633=DIRECTION ( 'NONE',  ( -0.000000000000000000, 0.3543493200069153248, 0.9351131265310292928 ) ) ;
#34635=AXIS2_PLACEMENT_3D ( 'NONE', #71608, #13622, #104190 ) ;
#34636=EDGE_CURVE ( 'NONE', #121050, #96774, #102169, .T. ) ;
#34637=FACE_OUTER_BOUND ( 'NONE', #23926, .T. ) ;
#34640=EDGE_CURVE ( 'NONE', #12475, #25213, #52676, .T. ) ;
#34642=DIRECTION ( 'NONE',  ( 0.7071067811865486830, -0.7071067811865464625, -0.000000000000000000 ) ) ;
#34643=ORIENTED_EDGE ( 'NONE', *, *, #132387, .T. ) ;
#34646=CARTESIAN_POINT ( 'NONE',  ( 0.000000000000000000, 0.000000000000000000, 5.000000000000000000 ) ) ;
#34647=DIRECTION ( 'NONE',  ( 0.7071067811865487940, 0.7071067811865463515, -0.000000000000000000 ) ) ;
#34648=AXIS2_PLACEMENT_3D ( 'NONE', #62980, #18701, #141209 ) ;
#34649=CARTESIAN_POINT ( 'NONE',  ( -9.280019679893985796, 0.7592924766157034266, 14.27032725228007060 ) ) ;
#34651=EDGE_CURVE ( 'NONE', #76579, #51133, #69552, .T. ) ;
#34652=VERTEX_POINT ( 'NONE', #14432 ) ;
#34653=ORIENTED_EDGE ( 'NONE', *, *, #112277, .T. ) ;
#34654=ORIENTED_EDGE ( 'NONE', *, *, #38288, .T. ) ;
#34656=ORIENTED_EDGE ( 'NONE', *, *, #132523, .T. ) ;
#34660=VECTOR ( 'NONE', #35344, 1000.000000000000000 ) ;
#34661=CARTESIAN_POINT ( 'NONE',  ( 34.92499999999998295, -22.22500000000000142, 4.500000000000000888 ) ) ;
#34665=CARTESIAN_POINT ( 'NONE',  ( -34.92500000000001137, 8.947904407527545345, 10.03118784388416351 ) ) ;
#34666=EDGE_CURVE ( 'NONE', #142228, #73248, #83254, .T. ) ;
#34667=CARTESIAN_POINT ( 'NONE',  ( 0.3281693992235254487, -12.74070752338415602, 4.000000000000000000 ) ) ;
#34669=EDGE_LOOP ( 'NONE', ( #122909, #30005, #58726, #87315 ) ) ;
#34670=DIRECTION ( 'NONE',  ( 0.7071067811865487940, 0.7071067811865463515, 0.000000000000000000 ) ) ;
#34671=LINE ( 'NONE', #112929, #37708 ) ;
#34673=EDGE_CURVE ( 'NONE', #123961, #74602, #26726, .T. ) ;
#34674=VECTOR ( 'NONE', #127125, 1000.000000000000000 ) ;
#34675=VECTOR ( 'NONE', #36905, 1000.000000000000227 ) ;
#34676=ORIENTED_EDGE ( 'NONE', *, *, #78841, .T. ) ;
#34677=VERTEX_POINT ( 'NONE', #4190 ) ;
#34678=CARTESIAN_POINT ( 'NONE',  ( 48.48921356237309510, -27.52281430457089328, 5.000000000000000000 ) ) ;
#34679=CIRCLE ( 'NONE', #87961, 0.5000000000000004441 ) ;
#34682=CIRCLE ( 'NONE', #53183, 5.968999999999998529 ) ;
#34683=ADVANCED_FACE ( 'NONE', ( #138351 ), #92678, .T. ) ;
#34684=LINE ( 'NONE', #2743, #94226 ) ;
#34685=PLANE ( 'NONE',  #11743 ) ;
#34686=CARTESIAN_POINT ( 'NONE',  ( -6.851816449618514326, 17.25929247661554555, 8.802941693769186671 ) ) ;
#34688=ORIENTED_EDGE ( 'NONE', *, *, #26492, .F. ) ;
#34689=ORIENTED_EDGE ( 'NONE', *, *, #55950, .T. ) ;
#34690=CARTESIAN_POINT ( 'NONE',  ( -11.51078643762690490, -27.52281430457047406, 5.000000000000000000 ) ) ;
#34691=ORIENTED_EDGE ( 'NONE', *, *, #122830, .F. ) ;
#34692=VERTEX_POINT ( 'NONE', #61537 ) ;
#34693=EDGE_CURVE ( 'NONE', #124198, #107914, #60089, .T. ) ;
#34694=VECTOR ( 'NONE', #10510, 1000.000000000000000 ) ;
#34695=EDGE_CURVE ( 'NONE', #96522, #83686, #70968, .T. ) ;
#34696=LINE ( 'NONE', #135446, #47443 ) ;
#34697=ORIENTED_EDGE ( 'NONE', *, *, #129435, .F. ) ;
#34698=DIRECTION ( 'NONE',  ( 0.7071067811865487940, -0.7071067811865463515, 0.000000000000000000 ) ) ;
#34699=DIRECTION ( 'NONE',  ( -0.7071067811865486830, -0.7071067811865464625, 0.000000000000000000 ) ) ;
#34700=EDGE_CURVE ( 'NONE', #95585, #72440, #93415, .T. ) ;
#34701=LINE ( 'NONE', #33308, #25202 ) ;
#34702=DIRECTION ( 'NONE',  ( -0.000000000000000000, 0.000000000000000000, 1.000000000000000000 ) ) ;
#34704=EDGE_CURVE ( 'NONE', #17089, #57042, #82542, .T. ) ;
#34706=ORIENTED_EDGE ( 'NONE', *, *, #53365, .F. ) ;
#34708=EDGE_LOOP ( 'NONE', ( #108473, #121347, #91424, #38421 ) ) ;
#34709=PLANE ( 'NONE',  #60834 ) ;
#34710=ORIENTED_EDGE ( 'NONE', *, *, #31790, .F. ) ;
#34711=CARTESIAN_POINT ( 'NONE',  ( 12.18398860626900060, 28.73617430169795739, 5.000000000000000000 ) ) ;
#34712=ORIENTED_EDGE ( 'NONE', *, *, #101230, .F. ) ;
#34713=ORIENTED_EDGE ( 'NONE', *, *, #103078, .T. ) ;
#34714=VERTEX_POINT ( 'NONE', #26025 ) ;
#34715=CARTESIAN_POINT ( 'NONE',  ( -60.48921356237309510, -27.52281430457097500, 5.000000000000000000 ) ) ;
#34717=DIRECTION ( 'NONE',  ( -0.3543493200069162685, -0.000000000000000000, -0.9351131265310288487 ) ) ;
#34720=EDGE_CURVE ( 'NONE', #122031, #100841, #39032, .T. ) ;
#34721=DIRECTION ( 'NONE',  ( 0.7071067811865487940, 0.7071067811865463515, -0.000000000000000000 ) ) ;
#34722=DIRECTION ( 'NONE',  ( 0.6830127018922181881, 0.6830127018922202975, -0.2588190451025214056 ) ) ;
#34725=LINE ( 'NONE', #78964, #23884 ) ;
#34727=ORIENTED_EDGE ( 'NONE', *, *, #119868, .T. ) ;
#34729=DIRECTION ( 'NONE',  ( -0.7071067811865486830, -0.7071067811865464625, 0.000000000000000000 ) ) ;
#34730=LINE ( 'NONE', #78970, #40228 ) ;
#34731=VERTEX_POINT ( 'NONE', #49929 ) ;
#34732=ORIENTED_EDGE ( 'NONE', *, *, #57465, .T. ) ;
#34733=AXIS2_PLACEMENT_3D ( 'NONE', #46659, #90849, #135079 ) ;
#34734=LINE ( 'NONE', #132652, #142096 ) ;
#34735=VECTOR ( 'NONE', #31177, 1000.000000000000000 ) ;
#34736=AXIS2_PLACEMENT_3D ( 'NONE', #136380, #92875, #82047 ) ;
#34737=ORIENTED_EDGE ( 'NONE', *, *, #82221, .F. ) ;
#34738=EDGE_LOOP ( 'NONE', ( #3605, #61002, #109732, #93844 ) ) ;
#34739=CARTESIAN_POINT ( 'NONE',  ( 0.000000000000000000, 21.72500000000000142, 4.500000000000000888 ) ) ;
#34742=CARTESIAN_POINT ( 'NONE',  ( -11.99999999999991473, -19.22509904557637839, 1.855685503482151111 ) ) ;
#34743=CARTESIAN_POINT ( 'NONE',  ( -32.99451991528749062, 28.92564299267960948, 4.000000000000000000 ) ) ;
#34744=ADVANCED_FACE ( 'NONE', ( #73114 ), #126059, .F. ) ;
#34745=VERTEX_POINT ( 'NONE', #115123 ) ;
#34746=CARTESIAN_POINT ( 'NONE',  ( 27.48921356237309155, -27.52281430457074762, 5.000000000000000000 ) ) ;
#34747=VECTOR ( 'NONE', #27648, 1000.000000000000000 ) ;
#34748=VERTEX_POINT ( 'NONE', #6347 ) ;
#34749=DIRECTION ( 'NONE',  ( 0.6830127018922180770, -0.6830127018922204085, -0.2588190451025213501 ) ) ;
#34750=ADVANCED_FACE ( 'NONE', ( #104258 ), #17952, .F. ) ;
#34752=ORIENTED_EDGE ( 'NONE', *, *, #66926, .F. ) ;
#34755=PLANE ( 'NONE',  #85931 ) ;
#34756=ORIENTED_EDGE ( 'NONE', *, *, #135187, .T. ) ;
#34757=ORIENTED_EDGE ( 'NONE', *, *, #61214, .F. ) ;
#34759=CARTESIAN_POINT ( 'NONE',  ( -27.32816939922334143, -21.74070752338406365, 4.000000000000000000 ) ) ;
#34760=VECTOR ( 'NONE', #129261, 1000.000000000000000 ) ;
#34762=CARTESIAN_POINT ( 'NONE',  ( -3.781626882924915112, 21.74787736706806385, 4.999607392498048419 ) ) ;
#34763=CARTESIAN_POINT ( 'NONE',  ( 34.92499999999998295, -5.143876922607530489, 4.000000000000000000 ) ) ;
#34764=ORIENTED_EDGE ( 'NONE', *, *, #102296, .T. ) ;
#34765=ADVANCED_FACE ( 'NONE', ( #3515 ), #47809, .F. ) ;
#34766=LINE ( 'NONE', #68149, #89735 ) ;
#34767=VECTOR ( 'NONE', #104706, 1000.000000000000000 ) ;
#34768=EDGE_CURVE ( 'NONE', #124632, #100584, #36876, .T. ) ;
#34769=LINE ( 'NONE', #23125, #65173 ) ;
#34770=DIRECTION ( 'NONE',  ( -0.7071067811865486830, -0.7071067811865464625, 0.000000000000000000 ) ) ;
#34771=VECTOR ( 'NONE', #54085, 1000.000000000000227 ) ;
#34773=DIRECTION ( 'NONE',  ( 0.7071067811865487940, 0.7071067811865463515, 0.000000000000000000 ) ) ;
#34775=VECTOR ( 'NONE', #105730, 1000.000000000000000 ) ;
#34776=VERTEX_POINT ( 'NONE', #126730 ) ;
#34778=EDGE_LOOP ( 'NONE', ( #92042, #12006, #109054, #32530 ) ) ;
#34780=EDGE_CURVE ( 'NONE', #14374, #116655, #125338, .T. ) ;
#34781=VECTOR ( 'NONE', #97683, 999.9999999999998863 ) ;
#34783=VECTOR ( 'NONE', #40712, 1000.000000000000000 ) ;
#34784=CARTESIAN_POINT ( 'NONE',  ( 38.99451991528749062, 28.92564299267965211, 4.000000000000000000 ) ) ;
#34785=EDGE_LOOP ( 'NONE', ( #140331, #116704, #108839, #95473 ) ) ;
#34788=DIRECTION ( 'NONE',  ( 0.6830127018922180770, -0.6830127018922204085, -0.2588190451025213501 ) ) ;
#34789=CARTESIAN_POINT ( 'NONE',  ( 23.81601139373100295, 28.73617430169770870, 5.000000000000000000 ) ) ;
#34790=DIRECTION ( 'NONE',  ( -0.7071067811865487940, 0.7071067811865463515, -0.000000000000000000 ) ) ;
#34792=CARTESIAN_POINT ( 'NONE',  ( 34.75611968250419181, 5.812934254707337267, 4.955485411084878500 ) ) ;
#34793=CARTESIAN_POINT ( 'NONE',  ( -17.51078643762690845, -27.52281430457043143, 5.000000000000000000 ) ) ;
#34795=CARTESIAN_POINT ( 'NONE',  ( 9.328169399223462221, 20.25929247661551358, 4.000000000000000000 ) ) ;
#34797=VECTOR ( 'NONE', #79947, 1000.000000000000000 ) ;
#34799=CARTESIAN_POINT ( 'NONE',  ( -35.99451991528749772, 28.92564299267963079, 4.000000000000000000 ) ) ;
#34800=CARTESIAN_POINT ( 'NONE',  ( -25.49999999999982592, 9.431123077392085108, 4.000000000000000000 ) ) ;
#34801=CARTESIAN_POINT ( 'NONE',  ( -34.42500000000001137, -21.02281430457035682, 5.000000000000000000 ) ) ;
#34802=ORIENTED_EDGE ( 'NONE', *, *, #123242, .T. ) ;
#34803=ORIENTED_EDGE ( 'NONE', *, *, #65143, .T. ) ;
#34805=EDGE_LOOP ( 'NONE', ( #98551, #36831, #20279, #126457 ) ) ;
#34806=EDGE_LOOP ( 'NONE', ( #47901, #36740, #80686 ) ) ;
#34808=ADVANCED_FACE ( 'NONE', ( #16542 ), #104992, .F. ) ;
#34809=DIRECTION ( 'NONE',  ( 0.7071067811865487940, 0.7071067811865463515, 0.000000000000000000 ) ) ;
#34810=LINE ( 'NONE', #25332, #67249 ) ;
#34814=DIRECTION ( 'NONE',  ( -0.3543493200069162685, -0.000000000000000000, -0.9351131265310288487 ) ) ;
#34815=CARTESIAN_POINT ( 'NONE',  ( -6.411614905948260557, 22.22500000000000142, 4.777194822843818578 ) ) ;
#34816=DIRECTION ( 'NONE',  ( 0.3543493200069162685, -0.000000000000000000, -0.9351131265310288487 ) ) ;
#34817=CARTESIAN_POINT ( 'NONE',  ( 57.18398860626899705, 28.73617430169827358, 5.000000000000000000 ) ) ;
#34819=EDGE_CURVE ( 'NONE', #17816, #98498, #31029, .T. ) ;
#34820=EDGE_CURVE ( 'NONE', #120961, #26817, #53481, .T. ) ;
#34822=CARTESIAN_POINT ( 'NONE',  ( -23.99999999999983302, -4.068876922607771895, 4.000000000000000000 ) ) ;
#34823=CARTESIAN_POINT ( 'NONE',  ( -36.18398860626899705, 28.73617430169812437, 5.000000000000000000 ) ) ;
#34825=VECTOR ( 'NONE', #117832, 1000.000000000000000 ) ;
#34826=LINE ( 'NONE', #113797, #2910 ) ;
#34828=AXIS2_PLACEMENT_3D ( 'NONE', #4356, #36356, #125508 ) ;
#34830=DIRECTION ( 'NONE',  ( -0.000000000000000000, 0.000000000000000000, 1.000000000000000000 ) ) ;
#34831=ADVANCED_FACE ( 'NONE', ( #129589 ), #118720, .T. ) ;
#34832=EDGE_CURVE ( 'NONE', #45231, #142570, #120119, .T. ) ;
#34834=ORIENTED_EDGE ( 'NONE', *, *, #11832, .T. ) ;
#34836=EDGE_CURVE ( 'NONE', #81792, #86890, #96232, .T. ) ;
#34837=ORIENTED_EDGE ( 'NONE', *, *, #31255, .T. ) ;
#34838=EDGE_CURVE ( 'NONE', #47477, #142342, #107828, .T. ) ;
#34839=FACE_OUTER_BOUND ( 'NONE', #113308, .T. ) ;
#34843=DIRECTION ( 'NONE',  ( -0.000000000000000000, 0.3543493200069153248, 0.9351131265310292928 ) ) ;
#34844=PLANE ( 'NONE',  #106717 ) ;
#34845=VECTOR ( 'NONE', #140580, 1000.000000000000000 ) ;
#34846=ADVANCED_FACE ( 'NONE', ( #65090 ), #109281, .T. ) ;
#34847=VECTOR ( 'NONE', #122737, 1000.000000000000000 ) ;
#34849=ORIENTED_EDGE ( 'NONE', *, *, #61755, .F. ) ;
#34850=ORIENTED_EDGE ( 'NONE', *, *, #101254, .T. ) ;
#34851=AXIS2_PLACEMENT_3D ( 'NONE', #120655, #39015, #73098 ) ;
#34852=VECTOR ( 'NONE', #59569, 1000.000000000000000 ) ;
#34854=CARTESIAN_POINT ( 'NONE',  ( -33.70701326429281153, -21.74070752338405299, 4.999753212805220670 ) ) ;
#34858=EDGE_LOOP ( 'NONE', ( #84342, #71869, #46149, #106981 ) ) ;
#34859=ORIENTED_EDGE ( 'NONE', *, *, #82645, .F. ) ;
#34862=AXIS2_PLACEMENT_3D ( 'NONE', #26076, #123267, #47860 ) ;
#34863=EDGE_CURVE ( 'NONE', #140375, #77966, #74538, .T. ) ;
#34865=ORIENTED_EDGE ( 'NONE', *, *, #102259, .F. ) ;
#34867=VERTEX_POINT ( 'NONE', #97688 ) ;
#34868=ORIENTED_EDGE ( 'NONE', *, *, #134261, .F. ) ;
#34871=AXIS2_PLACEMENT_3D ( 'NONE', #97412, #52494, #41621 ) ;
#34872=EDGE_CURVE ( 'NONE', #122126, #113634, #52743, .T. ) ;
#34873=VECTOR ( 'NONE', #73405, 1000.000000000000000 ) ;
#34875=CARTESIAN_POINT ( 'NONE',  ( -16.64175702458850381, 15.75929247661555799, 19.34181609438703475 ) ) ;
#34876=ORIENTED_EDGE ( 'NONE', *, *, #23214, .T. ) ;
#34877=CARTESIAN_POINT ( 'NONE',  ( -34.92500000000001137, -22.22500000000000142, 4.500000000000000888 ) ) ;
#34878=EDGE_CURVE ( 'NONE', #27313, #111053, #128884, .T. ) ;
#34879=VECTOR ( 'NONE', #8868, 1000.000000000000000 ) ;
#34880=DIRECTION ( 'NONE',  ( -0.7071067811865486830, 0.7071067811865464625, 0.000000000000000000 ) ) ;
#34881=VECTOR ( 'NONE', #138910, 1000.000000000000227 ) ;
#34882=EDGE_CURVE ( 'NONE', #49135, #64365, #59153, .T. ) ;
#34883=CARTESIAN_POINT ( 'NONE',  ( -71.99451991528749772, 28.92564299267988304, 4.000000000000000000 ) ) ;
#34884=FACE_BOUND ( 'NONE', #46329, .T. ) ;
#34886=CARTESIAN_POINT ( 'NONE',  ( -19.49999999999986855, -14.56887692260766087, 4.000000000000000000 ) ) ;
#34888=AXIS2_PLACEMENT_3D ( 'NONE', #68653, #123750, #26556 ) ;
#34889=CARTESIAN_POINT ( 'NONE',  ( 9.489213562373095101, -27.52281430457062328, 5.000000000000000000 ) ) ;
#34890=PLANE ( 'NONE',  #64770 ) ;
#34891=ORIENTED_EDGE ( 'NONE', *, *, #64836, .F. ) ;
#34892=CARTESIAN_POINT ( 'NONE',  ( -15.48921356237309510, -27.52281430457066236, 5.000000000000000000 ) ) ;
#34893=ORIENTED_EDGE ( 'NONE', *, *, #74431, .T. ) ;
#34894=ORIENTED_EDGE ( 'NONE', *, *, #1260, .F. ) ;
#34895=EDGE_LOOP ( 'NONE', ( #130952, #130519, #60760, #38331 ) ) ;
#34897=VERTEX_POINT ( 'NONE', #86112 ) ;
#34901=ADVANCED_FACE ( 'NONE', ( #73803 ), #9152, .F. ) ;
#34902=EDGE_LOOP ( 'NONE', ( #67331, #141193, #33618, #128173 ) ) ;
#34903=PLANE ( 'NONE',  #44534 ) ;
#34906=CARTESIAN_POINT ( 'NONE',  ( -17.99451991528748351, 28.92564299267950645, 4.000000000000000000 ) ) ;
#34907=LINE ( 'NONE', #46530, #96756 ) ;
#34908=DIRECTION ( 'NONE',  ( -0.7071067811865486830, -0.7071067811865464625, 0.000000000000000000 ) ) ;
#34909=FACE_OUTER_BOUND ( 'NONE', #10388, .T. ) ;
#34911=ORIENTED_EDGE ( 'NONE', *, *, #13577, .T. ) ;
#34912=ORIENTED_EDGE ( 'NONE', *, *, #74157, .F. ) ;
#34914=ORIENTED_EDGE ( 'NONE', *, *, #109263, .T. ) ;
#34915=CARTESIAN_POINT ( 'NONE',  ( 75.48921356237309510, -27.52281430457107803, 5.000000000000000000 ) ) ;
#34916=ORIENTED_EDGE ( 'NONE', *, *, #9233, .F. ) ;
#34917=VERTEX_POINT ( 'NONE', #39189 ) ;
#34918=CARTESIAN_POINT ( 'NONE',  ( -19.05000000000000071, 3.174999999999997158, 4.000000000000000000 ) ) ;
#34919=EDGE_CURVE ( 'NONE', #127061, #72848, #103688, .T. ) ;
#34920=CARTESIAN_POINT ( 'NONE',  ( -39.48921356237310221, -27.52281430457082934, 5.000000000000000000 ) ) ;
#34921=ORIENTED_EDGE ( 'NONE', *, *, #96670, .F. ) ;
#34922=LINE ( 'NONE', #89979, #122857 ) ;
#34923=VECTOR ( 'NONE', #96609, 1000.000000000000000 ) ;
#34924=DIRECTION ( 'NONE',  ( -0.7071067811865487940, 0.7071067811865463515, 0.000000000000000000 ) ) ;
#34925=EDGE_CURVE ( 'NONE', #133913, #120495, #95693, .T. ) ;
#34927=DIRECTION ( 'NONE',  ( -0.7071067811865486830, -0.7071067811865464625, 0.000000000000000000 ) ) ;
#34930=CARTESIAN_POINT ( 'NONE',  ( 13.49999999999991473, 22.08746187583902199, 4.000000000000000000 ) ) ;
#34932=FACE_OUTER_BOUND ( 'NONE', #11263, .T. ) ;
#34933=LINE ( 'NONE', #100878, #106702 ) ;
#34934=CARTESIAN_POINT ( 'NONE',  ( 9.299744871391588674, -27.71228299555212971, 4.000000000000000000 ) ) ;
#34935=DIRECTION ( 'NONE',  ( 0.7071067811865487940, 0.7071067811865463515, 0.000000000000000000 ) ) ;
#34936=ORIENTED_EDGE ( 'NONE', *, *, #98211, .T. ) ;
#34937=FACE_OUTER_BOUND ( 'NONE', #73249, .T. ) ;
#34938=VERTEX_POINT ( 'NONE', #43464 ) ;
#34939=FACE_OUTER_BOUND ( 'NONE', #127444, .T. ) ;
#34941=CARTESIAN_POINT ( 'NONE',  ( 18.32816939922340183, -21.74070752338405654, 4.000000000000000000 ) ) ;
#34942=PLANE ( 'NONE',  #37973 ) ;
#34943=ORIENTED_EDGE ( 'NONE', *, *, #47196, .F. ) ;
#34944=EDGE_CURVE ( 'NONE', #128178, #106502, #52880, .T. ) ;
#34945=AXIS2_PLACEMENT_3D ( 'NONE', #105626, #137583, #38268 ) ;
#34947=VECTOR ( 'NONE', #88354, 1000.000000000000000 ) ;
#34949=DIRECTION ( 'NONE',  ( -0.7071067811865487940, 0.7071067811865463515, -0.000000000000000000 ) ) ;
#34950=DIRECTION ( 'NONE',  ( 0.6830127018922181881, 0.6830127018922202975, -0.2588190451025214056 ) ) ;
#34951=ORIENTED_EDGE ( 'NONE', *, *, #37463, .T. ) ;
#34952=VECTOR ( 'NONE', #82040, 999.9999999999998863 ) ;
#34953=AXIS2_PLACEMENT_3D ( 'NONE', #137663, #126740, #84692 ) ;
#34954=VECTOR ( 'NONE', #53290, 1000.000000000000227 ) ;
#34955=AXIS2_PLACEMENT_3D ( 'NONE', #31272, #64602, #9466 ) ;
#34956=DIRECTION ( 'NONE',  ( -0.7071067811865486830, -0.7071067811865464625, 0.000000000000000000 ) ) ;
#34957=VECTOR ( 'NONE', #110639, 1000.000000000000000 ) ;
#34959=DIRECTION ( 'NONE',  ( 0.7071067811865486830, -0.7071067811865464625, -0.000000000000000000 ) ) ;
#34960=DIRECTION ( 'NONE',  ( 1.000000000000000000, 0.000000000000000000, 0.000000000000000000 ) ) ;
#34962=ADVANCED_FACE ( 'NONE', ( #52190 ), #8637, .F. ) ;
#34963=EDGE_LOOP ( 'NONE', ( #77703, #105729, #85119, #103887 ) ) ;
#34964=DIRECTION ( 'NONE',  ( -0.6830127018922181881, 0.6830127018922202975, -0.2588190451025214056 ) ) ;
#34965=VECTOR ( 'NONE', #19300, 1000.000000000000000 ) ;
#34966=DIRECTION ( 'NONE',  ( -0.7071067811865487940, 0.7071067811865463515, 0.000000000000000000 ) ) ;
#34967=ORIENTED_EDGE ( 'NONE', *, *, #40447, .T. ) ;
#34968=LINE ( 'NONE', #79205, #140925 ) ;
#34969=DIRECTION ( 'NONE',  ( -0.3543493200069162685, -0.000000000000000000, -0.9351131265310288487 ) ) ;
#34970=VERTEX_POINT ( 'NONE', #117420 ) ;
#34971=VECTOR ( 'NONE', #50910, 999.9999999999998863 ) ;
#34972=LINE ( 'NONE', #24078, #60567 ) ;
#34973=DIRECTION ( 'NONE',  ( -0.7071067811865487940, 0.7071067811865463515, -0.000000000000000000 ) ) ;
#34974=CARTESIAN_POINT ( 'NONE',  ( 27.79996877983145609, 8.259292476615630818, 16.85664084051834877 ) ) ;
#34975=VECTOR ( 'NONE', #15637, 999.9999999999998863 ) ;
#34976=FACE_OUTER_BOUND ( 'NONE', #99631, .T. ) ;
#34977=DIRECTION ( 'NONE',  ( -0.7071067811865486830, 0.7071067811865464625, 0.000000000000000000 ) ) ;
#34978=DIRECTION ( 'NONE',  ( -0.7071067811865486830, -0.7071067811865464625, 0.000000000000000000 ) ) ;
#34979=ORIENTED_EDGE ( 'NONE', *, *, #41714, .F. ) ;
#34980=VECTOR ( 'NONE', #132782, 1000.000000000000000 ) ;
#34983=CARTESIAN_POINT ( 'NONE',  ( -2.816011393730999401, 28.73617430169785436, 5.000000000000000000 ) ) ;
#34984=VECTOR ( 'NONE', #81567, 1000.000000000000000 ) ;
#34985=ORIENTED_EDGE ( 'NONE', *, *, #11317, .T. ) ;
#34986=ORIENTED_EDGE ( 'NONE', *, *, #15494, .F. ) ;
#34987=AXIS2_PLACEMENT_3D ( 'NONE', #95493, #94067, #140433 ) ;
#34988=ORIENTED_EDGE ( 'NONE', *, *, #84863, .F. ) ;
#34989=CARTESIAN_POINT ( 'NONE',  ( -28.49999999999980105, 13.08746187583910725, 4.000000000000000000 ) ) ;
#34990=DIRECTION ( 'NONE',  ( -0.7071067811865486830, -0.7071067811865464625, -0.000000000000000000 ) ) ;
#34992=EDGE_LOOP ( 'NONE', ( #75728, #23561, #142727, #17805 ) ) ;
#34993=LINE ( 'NONE', #58200, #129532 ) ;
#34995=CARTESIAN_POINT ( 'NONE',  ( 51.48921356237309510, -27.52281430457091460, 5.000000000000000000 ) ) ;
#34996=DIRECTION ( 'NONE',  ( -0.7071067811865486830, 0.7071067811865464625, 0.000000000000000000 ) ) ;
#34999=VERTEX_POINT ( 'NONE', #32605 ) ;
#35000=LINE ( 'NONE', #113960, #136784 ) ;
#35002=DIRECTION ( 'NONE',  ( -0.3543493200069162685, -0.000000000000000000, -0.9351131265310288487 ) ) ;
#35004=CARTESIAN_POINT ( 'NONE',  ( 19.49999999999986855, -20.94781430457061333, 5.000000000000000000 ) ) ;
#35008=CARTESIAN_POINT ( 'NONE',  ( -32.99999999999977263, -21.84840872380827292, 2.849755605029529626 ) ) ;
#35009=ADVANCED_FACE ( 'NONE', ( #84825 ), #10110, .T. ) ;
#35010=CARTESIAN_POINT ( 'NONE',  ( 0.000000000000000000, 0.000000000000000000, 5.000000000000000000 ) ) ;
#35011=AXIS2_PLACEMENT_3D ( 'NONE', #101895, #54844, #111329 ) ;
#35012=ORIENTED_EDGE ( 'NONE', *, *, #43618, .T. ) ;
#35013=ORIENTED_EDGE ( 'NONE', *, *, #83532, .T. ) ;
#35015=EDGE_CURVE ( 'NONE', #136794, #89060, #86272, .T. ) ;
#35016=FACE_OUTER_BOUND ( 'NONE', #98969, .T. ) ;
#35017=EDGE_CURVE ( 'NONE', #142342, #20063, #30453, .T. ) ;
#35018=VECTOR ( 'NONE', #133944, 1000.000000000000227 ) ;
#35019=EDGE_LOOP ( 'NONE', ( #7167, #18923, #127586, #101175 ) ) ;
#35020=AXIS2_PLACEMENT_3D ( 'NONE', #131766, #55635, #88985 ) ;
#35021=EDGE_CURVE ( 'NONE', #137395, #3235, #29707, .T. ) ;
#35022=DIRECTION ( 'NONE',  ( -0.3543493200069162685, -0.000000000000000000, -0.9351131265310288487 ) ) ;
#35023=DIRECTION ( 'NONE',  ( 0.6830127018922180770, -0.6830127018922204085, -0.2588190451025213501 ) ) ;
#35025=ORIENTED_EDGE ( 'NONE', *, *, #141179, .F. ) ;
#35027=FACE_OUTER_BOUND ( 'NONE', #21893, .T. ) ;
#35028=ORIENTED_EDGE ( 'NONE', *, *, #8932, .F. ) ;
#35029=CARTESIAN_POINT ( 'NONE',  ( 28.82816939922333432, 12.75929247661558996, 4.000000000000000000 ) ) ;
#35030=LINE ( 'NONE', #36435, #8323 ) ;
#35033=CARTESIAN_POINT ( 'NONE',  ( -14.72063736826144087, 7.288814752023359489, 4.957798599204234158 ) ) ;
#35034=ORIENTED_EDGE ( 'NONE', *, *, #135478, .T. ) ;
#35035=EDGE_CURVE ( 'NONE', #90903, #87458, #65244, .T. ) ;
#35037=EDGE_LOOP ( 'NONE', ( #86121, #134701, #85816, #85504, #9042 ) ) ;
#35038=FACE_OUTER_BOUND ( 'NONE', #43601, .T. ) ;
#35039=CARTESIAN_POINT ( 'NONE',  ( -31.00193056682077497, -22.22500000000000142, 4.500000000000000888 ) ) ;
#35040=DIRECTION ( 'NONE',  ( -0.6830127018922181881, 0.6830127018922202975, -0.2588190451025214056 ) ) ;
#35041=CARTESIAN_POINT ( 'NONE',  ( 25.49999999999982236, -12.08601207473286543, -10.46905243149100251 ) ) ;
#35043=EDGE_CURVE ( 'NONE', #23765, #32169, #109429, .T. ) ;
#35044=VERTEX_POINT ( 'NONE', #67380 ) ;
#35045=DIRECTION ( 'NONE',  ( -0.3543493200069162685, -0.000000000000000000, -0.9351131265310288487 ) ) ;
#35047=PLANE ( 'NONE',  #41863 ) ;
#35048=LINE ( 'NONE', #66942, #133485 ) ;
#35049=CARTESIAN_POINT ( 'NONE',  ( -33.18398860626899705, 28.73617430169810305, 5.000000000000000000 ) ) ;
#35051=ORIENTED_EDGE ( 'NONE', *, *, #82608, .F. ) ;
#35052=DIRECTION ( 'NONE',  ( 0.7071067811865487940, 0.7071067811865463515, -0.000000000000000000 ) ) ;
#35054=ORIENTED_EDGE ( 'NONE', *, *, #6792, .T. ) ;
#35057=PLANE ( 'NONE',  #46593 ) ;
#35058=ORIENTED_EDGE ( 'NONE', *, *, #10689, .F. ) ;
#35059=DIRECTION ( 'NONE',  ( 0.000000000000000000, 0.000000000000000000, 1.000000000000000000 ) ) ;
#35060=DIRECTION ( 'NONE',  ( -0.7071067811865487940, 0.7071067811865463515, -0.000000000000000000 ) ) ;
#35061=EDGE_CURVE ( 'NONE', #23219, #19313, #13657, .T. ) ;
#35063=VECTOR ( 'NONE', #98265, 1000.000000000000227 ) ;
#35066=AXIS2_PLACEMENT_3D ( 'NONE', #77021, #64696, #21889 ) ;
#35068=FACE_BOUND ( 'NONE', #57070, .T. ) ;
#35069=LINE ( 'NONE', #68419, #13270 ) ;
#35070=DIRECTION ( 'NONE',  ( 0.7071067811865487940, -0.7071067811865463515, 0.000000000000000000 ) ) ;
#35071=DIRECTION ( 'NONE',  ( 1.000000000000000000, 0.000000000000000000, 0.000000000000000000 ) ) ;
#35072=DIRECTION ( 'NONE',  ( 0.7071067811865487940, 0.7071067811865463515, -0.000000000000000000 ) ) ;
#35073=ORIENTED_EDGE ( 'NONE', *, *, #84859, .F. ) ;
#35074=LINE ( 'NONE', #33643, #143532 ) ;
#35075=VERTEX_POINT ( 'NONE', #132656 ) ;
#35076=ORIENTED_EDGE ( 'NONE', *, *, #120715, .F. ) ;
#35078=ORIENTED_EDGE ( 'NONE', *, *, #12027, .T. ) ;
#35079=VECTOR ( 'NONE', #47573, 1000.000000000000000 ) ;
#35080=CARTESIAN_POINT ( 'NONE',  ( -18.18398860626898994, 28.73617430169800002, 5.000000000000000000 ) ) ;
#35082=VERTEX_POINT ( 'NONE', #134055 ) ;
#35083=PLANE ( 'NONE',  #56013 ) ;
#35085=AXIS2_PLACEMENT_3D ( 'NONE', #50702, #95621, #128273 ) ;
#35086=CARTESIAN_POINT ( 'NONE',  ( -32.99999999999976552, -16.44781430457067373, 5.000000000000000000 ) ) ;
#35087=EDGE_CURVE ( 'NONE', #74042, #91540, #10799, .T. ) ;
#35089=CARTESIAN_POINT ( 'NONE',  ( 0.000000000000000000, 0.000000000000000000, 5.000000000000000000 ) ) ;
#35091=DIRECTION ( 'NONE',  ( 0.7071067811865487940, 0.7071067811865463515, -0.000000000000000000 ) ) ;
#35092=LINE ( 'NONE', #114738, #9215 ) ;
#35093=ORIENTED_EDGE ( 'NONE', *, *, #116605, .T. ) ;
#35094=ORIENTED_EDGE ( 'NONE', *, *, #123556, .F. ) ;
#35096=DIRECTION ( 'NONE',  ( 0.6830127018922180770, -0.6830127018922204085, -0.2588190451025213501 ) ) ;
#35097=CARTESIAN_POINT ( 'NONE',  ( -18.32816939922339472, -3.740707523384251942, 4.000000000000000000 ) ) ;
#35098=EDGE_LOOP ( 'NONE', ( #96443, #41341, #19082, #125665 ) ) ;
#35099=EDGE_LOOP ( 'NONE', ( #17282, #135994, #65781, #42920 ) ) ;
#35100=ORIENTED_EDGE ( 'NONE', *, *, #89012, .T. ) ;
#35101=ADVANCED_FACE ( 'NONE', ( #68122 ), #79718, .F. ) ;
#35102=VECTOR ( 'NONE', #100909, 1000.000000000000000 ) ;
#35104=VERTEX_POINT ( 'NONE', #134789 ) ;
#35105=FACE_OUTER_BOUND ( 'NONE', #72174, .T. ) ;
#35106=LINE ( 'NONE', #135823, #30804 ) ;
#35108=DIRECTION ( 'NONE',  ( -0.000000000000000000, 0.3543493200069152138, -0.9351131265310292928 ) ) ;
#35109=VERTEX_POINT ( 'NONE', #88415 ) ;
#35110=DIRECTION ( 'NONE',  ( 0.7071067811865486830, -0.7071067811865464625, -0.000000000000000000 ) ) ;
#35111=CARTESIAN_POINT ( 'NONE',  ( -63.48921356237309510, -27.52281430457099631, 5.000000000000000000 ) ) ;
#35113=PLANE ( 'NONE',  #86815 ) ;
#35115=ORIENTED_EDGE ( 'NONE', *, *, #50913, .F. ) ;
#35116=VECTOR ( 'NONE', #34973, 999.9999999999998863 ) ;
#35117=VERTEX_POINT ( 'NONE', #45635 ) ;
#35120=ADVANCED_FACE ( 'NONE', ( #55067 ), #11507, .F. ) ;
#35121=CARTESIAN_POINT ( 'NONE',  ( 31.49999999999977973, -4.912538124160700015, 4.000000000000000000 ) ) ;
#35122=VERTEX_POINT ( 'NONE', #47097 ) ;
#35123=CARTESIAN_POINT ( 'NONE',  ( -72.48921356237309510, -27.52281430457106026, 5.000000000000000000 ) ) ;
#35124=EDGE_CURVE ( 'NONE', #94490, #49817, #78979, .T. ) ;
#35125=VECTOR ( 'NONE', #83217, 1000.000000000000227 ) ;
#35126=CARTESIAN_POINT ( 'NONE',  ( -22.49999999999984013, -19.53360074219753884, 5.000000000000000000 ) ) ;
#35127=PLANE ( 'NONE',  #118086 ) ;
#35128=DIRECTION ( 'NONE',  ( -0.000000000000000000, 0.000000000000000000, 1.000000000000000000 ) ) ;
#35132=DIRECTION ( 'NONE',  ( 1.000000000000000000, 0.000000000000000000, 0.000000000000000000 ) ) ;
#35133=CARTESIAN_POINT ( 'NONE',  ( -5.700255128608413102, -27.71228299555201957, 4.000000000000000000 ) ) ;
#35135=CARTESIAN_POINT ( 'NONE',  ( -32.29289321881323360, 2.259292476615690770, 5.000000000000000000 ) ) ;
#35136=EDGE_LOOP ( 'NONE', ( #104426, #78643, #97443 ) ) ;
#35137=ADVANCED_FACE ( 'NONE', ( #2052 ), #90549, .F. ) ;
#35139=VECTOR ( 'NONE', #16764, 1000.000000000000000 ) ;
#35141=CARTESIAN_POINT ( 'NONE',  ( -4.499999999999972466, 6.277155672890267546, -3.510561720658931684 ) ) ;
#35142=DIRECTION ( 'NONE',  ( -0.000000000000000000, 0.000000000000000000, 1.000000000000000000 ) ) ;
#35144=ORIENTED_EDGE ( 'NONE', *, *, #102065, .F. ) ;
#35145=CARTESIAN_POINT ( 'NONE',  ( 24.18398860626899705, 28.73617430169804265, 5.000000000000000000 ) ) ;
#35146=CARTESIAN_POINT ( 'NONE',  ( 32.99999999999977973, 1.931123077392167264, 4.000000000000000000 ) ) ;
#35147=LINE ( 'NONE', #101076, #25918 ) ;
#35148=VERTEX_POINT ( 'NONE', #68811 ) ;
#35149=LINE ( 'NONE', #36547, #134439 ) ;
#35150=LINE ( 'NONE', #34411, #121022 ) ;
#35151=VECTOR ( 'NONE', #11345, 1000.000000000000000 ) ;
#35153=PLANE ( 'NONE',  #124614 ) ;
#35156=DIRECTION ( 'NONE',  ( 0.6830127018922181881, 0.6830127018922202975, -0.2588190451025214056 ) ) ;
#35157=AXIS2_PLACEMENT_3D ( 'NONE', #40951, #64135, #75727 ) ;
#35160=CARTESIAN_POINT ( 'NONE',  ( -20.81601139373100295, 28.73617430169773002, 5.000000000000000000 ) ) ;
#35161=ORIENTED_EDGE ( 'NONE', *, *, #48069, .T. ) ;
#35163=EDGE_LOOP ( 'NONE', ( #45454, #26347, #5081, #135934 ) ) ;
#35164=VECTOR ( 'NONE', #123028, 1000.000000000000227 ) ;
#35165=VECTOR ( 'NONE', #101277, 1000.000000000000000 ) ;
#35167=VECTOR ( 'NONE', #49841, 1000.000000000000227 ) ;
#35169=DIRECTION ( 'NONE',  ( 0.7071067811865487940, -0.7071067811865463515, 0.000000000000000000 ) ) ;
#35170=DIRECTION ( 'NONE',  ( -0.6830127018922181881, 0.6830127018922202975, -0.2588190451025214056 ) ) ;
#35171=DIRECTION ( 'NONE',  ( -0.7071067811865487940, 0.7071067811865463515, -0.000000000000000000 ) ) ;
#35172=PLANE ( 'NONE',  #52320 ) ;
#35173=EDGE_LOOP ( 'NONE', ( #56787, #106694, #18224, #27931, #82472 ) ) ;
#35174=ORIENTED_EDGE ( 'NONE', *, *, #136943, .F. ) ;
#35175=LINE ( 'NONE', #103935, #39436 ) ;
#35177=DIRECTION ( 'NONE',  ( -0.000000000000000000, -0.3543493200069152693, 0.9351131265310292928 ) ) ;
#35178=LINE ( 'NONE', #101832, #131391 ) ;
#35180=CARTESIAN_POINT ( 'NONE',  ( 15.48921356237309510, -27.52281430457066236, 5.000000000000000000 ) ) ;
#35181=ADVANCED_FACE ( 'NONE', ( #105663 ), #17253, .T. ) ;
#35182=CARTESIAN_POINT ( 'NONE',  ( 1.213219033033586136, 12.75929247661558996, 10.29404684609035492 ) ) ;
#35183=ORIENTED_EDGE ( 'NONE', *, *, #75867, .F. ) ;
#35185=FACE_OUTER_BOUND ( 'NONE', #65926, .T. ) ;
#35186=EDGE_CURVE ( 'NONE', #120060, #77465, #136176, .T. ) ;
#35187=DIRECTION ( 'NONE',  ( 0.7071067811865487940, 0.7071067811865463515, -0.000000000000000000 ) ) ;
#35188=CARTESIAN_POINT ( 'NONE',  ( -51.48921356237309510, -27.52281430457091460, 5.000000000000000000 ) ) ;
#35189=EDGE_LOOP ( 'NONE', ( #70584, #5601, #56491, #108282 ) ) ;
#35190=EDGE_CURVE ( 'NONE', #106541, #82440, #48456, .T. ) ;
#35191=EDGE_CURVE ( 'NONE', #103105, #56655, #25999, .T. ) ;
#35192=VECTOR ( 'NONE', #27355, 1000.000000000000000 ) ;
#35193=DIRECTION ( 'NONE',  ( 0.7071067811865487940, -0.7071067811865463515, 0.000000000000000000 ) ) ;
#35195=CARTESIAN_POINT ( 'NONE',  ( -2.510786437626908008, -27.52281430457053446, 5.000000000000000000 ) ) ;
#35197=VECTOR ( 'NONE', #7046, 1000.000000000000227 ) ;
#35198=ORIENTED_EDGE ( 'NONE', *, *, #59925, .F. ) ;
#35199=ORIENTED_EDGE ( 'NONE', *, *, #60241, .F. ) ;
#35200=VECTOR ( 'NONE', #96116, 1000.000000000000000 ) ;
#35201=LINE ( 'NONE', #79445, #112386 ) ;
#35202=FACE_OUTER_BOUND ( 'NONE', #16111, .T. ) ;
#35204=CARTESIAN_POINT ( 'NONE',  ( -20.99999999999984368, -22.22500000000000142, 4.412002311790043763 ) ) ;
#35206=DIRECTION ( 'NONE',  ( 0.7071067811865487940, 0.7071067811865463515, 0.000000000000000000 ) ) ;
#35208=ORIENTED_EDGE ( 'NONE', *, *, #123890, .T. ) ;
#35209=PLANE ( 'NONE',  #48415 ) ;
#35210=DIRECTION ( 'NONE',  ( 0.3543493200069162685, -0.000000000000000000, -0.9351131265310288487 ) ) ;
#35211=CARTESIAN_POINT ( 'NONE',  ( 0.7928932188134545367, 0.7592924766157086447, 5.000000000000000000 ) ) ;
#35212=VECTOR ( 'NONE', #25765, 1000.000000000000000 ) ;
#35213=CARTESIAN_POINT ( 'NONE',  ( -30.32816939922330945, -12.74070752338414891, 4.000000000000000000 ) ) ;
#35214=ORIENTED_EDGE ( 'NONE', *, *, #116159, .T. ) ;
#35216=ORIENTED_EDGE ( 'NONE', *, *, #122793, .T. ) ;
#35218=ORIENTED_EDGE ( 'NONE', *, *, #36030, .T. ) ;
#35219=CARTESIAN_POINT ( 'NONE',  ( 18.48921356237309510, -27.52281430457068367, 5.000000000000000000 ) ) ;
#35220=LINE ( 'NONE', #56279, #43285 ) ;
#35221=VECTOR ( 'NONE', #18753, 1000.000000000000000 ) ;
#35222=FACE_OUTER_BOUND ( 'NONE', #101527, .T. ) ;
#35224=ORIENTED_EDGE ( 'NONE', *, *, #37226, .F. ) ;
#35225=VERTEX_POINT ( 'NONE', #82520 ) ;
#35227=AXIS2_PLACEMENT_3D ( 'NONE', #140500, #129622, #9231 ) ;
#35230=ORIENTED_EDGE ( 'NONE', *, *, #60401, .F. ) ;
#35231=CARTESIAN_POINT ( 'NONE',  ( -1.591674519009985467, -0.7407075233842770334, 14.76736230305380282 ) ) ;
#35232=DIRECTION ( 'NONE',  ( 0.7071067811865487940, 0.7071067811865463515, 0.000000000000000000 ) ) ;
#35233=EDGE_CURVE ( 'NONE', #52005, #10836, #125311, .T. ) ;
#35234=LINE ( 'NONE', #22861, #58543 ) ;
#35235=VECTOR ( 'NONE', #16739, 1000.000000000000227 ) ;
#35236=( BOUNDED_CURVE ( )  B_SPLINE_CURVE ( 3, ( #56988, #112759, #57700, #101879 ),
 .UNSPECIFIED., .F., .T. ) 
 B_SPLINE_CURVE_WITH_KNOTS ( ( 4, 4 ),
 ( 1.500914606003787677, 1.515984175831967429 ),
 .UNSPECIFIED. ) 
 CURVE ( )  GEOMETRIC_REPRESENTATION_ITEM ( )  RATIONAL_B_SPLINE_CURVE ( ( 1.000000000000000000, 0.9999810757616318657, 0.9999810757616318657, 1.000000000000000000 ) ) 
 REPRESENTATION_ITEM ( '' )  );
#35237=ORIENTED_EDGE ( 'NONE', *, *, #109620, .T. ) ;
#35238=FACE_BOUND ( 'NONE', #66414, .T. ) ;
#35242=LINE ( 'NONE', #114191, #64432 ) ;
#35243=EDGE_CURVE ( 'NONE', #37784, #112545, #59367, .T. ) ;
#35244=LINE ( 'NONE', #36628, #119769 ) ;
#35245=CARTESIAN_POINT ( 'NONE',  ( -10.82816939922345689, -2.240707523384257716, 4.000000000000000000 ) ) ;
#35247=ADVANCED_FACE ( 'NONE', ( #37597 ), #70945, .F. ) ;
#35248=ORIENTED_EDGE ( 'NONE', *, *, #22202, .F. ) ;
#35249=VERTEX_POINT ( 'NONE', #81842 ) ;
#35251=ORIENTED_EDGE ( 'NONE', *, *, #129310, .T. ) ;
#35252=DIRECTION ( 'NONE',  ( 0.7071067811865487940, -0.7071067811865463515, 0.000000000000000000 ) ) ;
#35253=VERTEX_POINT ( 'NONE', #15773 ) ;
#35254=CARTESIAN_POINT ( 'NONE',  ( 26.99999999999981881, -3.485240976185050243, -4.108735105802335141 ) ) ;
#35256=AXIS2_PLACEMENT_3D ( 'NONE', #44206, #55075, #99243 ) ;
#35257=VECTOR ( 'NONE', #87617, 1000.000000000000000 ) ;
#35261=DIRECTION ( 'NONE',  ( 0.6830127018922181881, 0.6830127018922202975, -0.2588190451025214056 ) ) ;
#35262=ORIENTED_EDGE ( 'NONE', *, *, #65668, .T. ) ;
#35263=CARTESIAN_POINT ( 'NONE',  ( -37.82334089840004054, 5.259292476615672562, 15.86257073897106729 ) ) ;
#35264=CARTESIAN_POINT ( 'NONE',  ( -20.67183060077632106, -3.740707523384244837, 4.000000000000000000 ) ) ;
#35265=EDGE_CURVE ( 'NONE', #76165, #51777, #104236, .T. ) ;
#35267=LINE ( 'NONE', #102649, #41088 ) ;
#35268=CARTESIAN_POINT ( 'NONE',  ( -2.999999999999978240, 2.342191155542447500, -5.001666872980077727 ) ) ;
#35269=LINE ( 'NONE', #79509, #78616 ) ;
#35270=AXIS2_PLACEMENT_3D ( 'NONE', #122885, #67839, #101121 ) ;
#35271=AXIS2_PLACEMENT_3D ( 'NONE', #68360, #54602, #159 ) ;
#35274=ORIENTED_EDGE ( 'NONE', *, *, #12746, .T. ) ;
#35275=LINE ( 'NONE', #24357, #33423 ) ;
#35276=CARTESIAN_POINT ( 'NONE',  ( 2.510786437626908008, -27.52281430457053446, 5.000000000000000000 ) ) ;
#35277=EDGE_LOOP ( 'NONE', ( #125027, #134681, #137717, #129416 ) ) ;
#35278=ORIENTED_EDGE ( 'NONE', *, *, #130147, .F. ) ;
#35280=ORIENTED_EDGE ( 'NONE', *, *, #76529, .T. ) ;
#35286=CARTESIAN_POINT ( 'NONE',  ( -20.72174548431414465, 8.259292476615634371, 11.78515199841145744 ) ) ;
#35287=ORIENTED_EDGE ( 'NONE', *, *, #2129, .F. ) ;
#35288=CARTESIAN_POINT ( 'NONE',  ( -60.29974487139158867, -27.71228299555248142, 4.000000000000000000 ) ) ;
#35289=ORIENTED_EDGE ( 'NONE', *, *, #120926, .F. ) ;
#35291=FACE_OUTER_BOUND ( 'NONE', #8439, .T. ) ;
#35292=ORIENTED_EDGE ( 'NONE', *, *, #60290, .F. ) ;
#35293=VECTOR ( 'NONE', #39171, 1000.000000000000227 ) ;
#35294=CARTESIAN_POINT ( 'NONE',  ( -23.99451991528749062, 28.92564299267954908, 4.000000000000000000 ) ) ;
#35296=ORIENTED_EDGE ( 'NONE', *, *, #137292, .F. ) ;
#35297=FACE_OUTER_BOUND ( 'NONE', #120784, .T. ) ;
#35299=VERTEX_POINT ( 'NONE', #52033 ) ;
#35300=EDGE_LOOP ( 'NONE', ( #52579, #117382, #40455, #7968 ) ) ;
#35301=ORIENTED_EDGE ( 'NONE', *, *, #68463, .F. ) ;
#35302=DIRECTION ( 'NONE',  ( -0.7071067811865487940, 0.7071067811865463515, -0.000000000000000000 ) ) ;
#35304=DIRECTION ( 'NONE',  ( -0.7071067811865486830, -0.7071067811865464625, 0.000000000000000000 ) ) ;
#35305=LINE ( 'NONE', #79547, #121142 ) ;
#35306=EDGE_CURVE ( 'NONE', #26996, #86210, #119395, .T. ) ;
#35307=DIRECTION ( 'NONE',  ( 0.7071067811865487940, 0.7071067811865463515, 0.000000000000000000 ) ) ;
#35308=EDGE_CURVE ( 'NONE', #93715, #64105, #138723, .T. ) ;
#35309=CARTESIAN_POINT ( 'NONE',  ( -8.999999999999952038, 17.58746187583908238, 4.000000000000000000 ) ) ;
#35310=ORIENTED_EDGE ( 'NONE', *, *, #133971, .T. ) ;
#35311=VECTOR ( 'NONE', #78394, 1000.000000000000114 ) ;
#35312=LINE ( 'NONE', #23685, #119076 ) ;
#35314=CARTESIAN_POINT ( 'NONE',  ( -5.700255128608413102, -27.71228299555201957, 4.000000000000000000 ) ) ;
#35315=CARTESIAN_POINT ( 'NONE',  ( -56.99451991528749062, 28.92564299267978001, 4.000000000000000000 ) ) ;
#35316=ADVANCED_FACE ( 'NONE', ( #128862 ), #28855, .F. ) ;
#35319=ORIENTED_EDGE ( 'NONE', *, *, #97449, .T. ) ;
#35320=AXIS2_PLACEMENT_3D ( 'NONE', #87269, #55367, #107576 ) ;
#35321=ORIENTED_EDGE ( 'NONE', *, *, #141882, .F. ) ;
#35322=CARTESIAN_POINT ( 'NONE',  ( 33.48921356237309510, -27.52281430457078670, 5.000000000000000000 ) ) ;
#35324=DIRECTION ( 'NONE',  ( -0.7071067811865487940, 0.7071067811865463515, 0.000000000000000000 ) ) ;
#35325=CARTESIAN_POINT ( 'NONE',  ( 24.79289321881329045, 0.7592924766157156391, 5.000000000000000000 ) ) ;
#35326=DIRECTION ( 'NONE',  ( -0.000000000000000000, 0.000000000000000000, 1.000000000000000000 ) ) ;
#35328=LINE ( 'NONE', #67972, #13629 ) ;
#35329=DIRECTION ( 'NONE',  ( -0.7071067811865487940, 0.7071067811865463515, 0.000000000000000000 ) ) ;
#35330=PLANE ( 'NONE',  #81425 ) ;
#35332=FACE_OUTER_BOUND ( 'NONE', #141339, .T. ) ;
#35333=VERTEX_POINT ( 'NONE', #96214 ) ;
#35334=EDGE_CURVE ( 'NONE', #84329, #88412, #53455, .T. ) ;
#35337=VERTEX_POINT ( 'NONE', #107107 ) ;
#35338=CARTESIAN_POINT ( 'NONE',  ( 60.48921356237309510, -27.52281430457097500, 5.000000000000000000 ) ) ;
#35339=LINE ( 'NONE', #81701, #53344 ) ;
#35340=ORIENTED_EDGE ( 'NONE', *, *, #121511, .T. ) ;
#35341=CARTESIAN_POINT ( 'NONE',  ( -54.48921356237310221, -27.52281430457093236, 5.000000000000000000 ) ) ;
#35342=DIRECTION ( 'NONE',  ( -0.7071067811865486830, -0.7071067811865464625, 0.000000000000000000 ) ) ;
#35343=EDGE_LOOP ( 'NONE', ( #58011, #18955, #81950, #33091 ) ) ;
#35344=DIRECTION ( 'NONE',  ( -0.000000000000000000, -0.3543493200069152693, 0.9351131265310292928 ) ) ;
#35345=VECTOR ( 'NONE', #74774, 1000.000000000000000 ) ;
#35346=VERTEX_POINT ( 'NONE', #7047 ) ;
#35347=FACE_OUTER_BOUND ( 'NONE', #25243, .T. ) ;
#35348=ORIENTED_EDGE ( 'NONE', *, *, #252, .F. ) ;
#35349=LINE ( 'NONE', #131783, #33731 ) ;
#35351=DIRECTION ( 'NONE',  ( -0.000000000000000000, 0.3543493200069153248, 0.9351131265310292928 ) ) ;
#35352=ORIENTED_EDGE ( 'NONE', *, *, #80849, .F. ) ;
#35353=CARTESIAN_POINT ( 'NONE',  ( -33.29974487139158867, -27.71228299555229313, 4.000000000000000000 ) ) ;
#35355=EDGE_CURVE ( 'NONE', #104658, #28238, #51327, .T. ) ;
#35356=DIRECTION ( 'NONE',  ( -0.3543493200069162685, -0.000000000000000000, -0.9351131265310288487 ) ) ;
#35358=LINE ( 'NONE', #56415, #58449 ) ;
#35359=VECTOR ( 'NONE', #108541, 1000.000000000000000 ) ;
#35360=VECTOR ( 'NONE', #64711, 1000.000000000000000 ) ;
#35361=AXIS2_PLACEMENT_3D ( 'NONE', #52490, #129333, #4106 ) ;
#35362=LINE ( 'NONE', #12837, #109255 ) ;
#35363=CARTESIAN_POINT ( 'NONE',  ( -29.28769006033951783, -21.73547319004780931, 4.999917730833664642 ) ) ;
#35365=EDGE_CURVE ( 'NONE', #95118, #97786, #17928, .T. ) ;
#35366=VECTOR ( 'NONE', #41682, 1000.000000000000000 ) ;
#35367=ADVANCED_FACE ( 'NONE', ( #18657 ), #11892, .F. ) ;
#35369=DIRECTION ( 'NONE',  ( 0.7071067811865486830, -0.7071067811865464625, -0.000000000000000000 ) ) ;
#35370=ORIENTED_EDGE ( 'NONE', *, *, #102664, .T. ) ;
#35372=CARTESIAN_POINT ( 'NONE',  ( -27.29974487139158512, -27.71228299555225405, 4.000000000000000000 ) ) ;
#35373=VECTOR ( 'NONE', #41408, 1000.000000000000000 ) ;
#35374=PLANE ( 'NONE',  #44706 ) ;
#35375=AXIS2_PLACEMENT_3D ( 'NONE', #69051, #36407, #113232 ) ;
#35377=CARTESIAN_POINT ( 'NONE',  ( 32.99999999999977263, 20.70535890316564220, 1.956823837851840775 ) ) ;
#35378=EDGE_LOOP ( 'NONE', ( #1026, #100507, #139416, #102264 ) ) ;
#35379=ADVANCED_FACE ( 'NONE', ( #95516 ), #107809, .F. ) ;
#35382=EDGE_CURVE ( 'NONE', #39036, #73921, #44591, .T. ) ;
#35383=ORIENTED_EDGE ( 'NONE', *, *, #15872, .F. ) ;
#35384=LINE ( 'NONE', #135401, #60134 ) ;
#35385=EDGE_CURVE ( 'NONE', #53474, #18032, #56182, .T. ) ;
#35386=DIRECTION ( 'NONE',  ( -0.6830127018922180770, -0.6830127018922204085, -0.2588190451025213501 ) ) ;
#35387=EDGE_LOOP ( 'NONE', ( #67695, #123178, #115947, #138924 ) ) ;
#35388=CARTESIAN_POINT ( 'NONE',  ( 78.18398860626899705, 28.73617430169841924, 5.000000000000000000 ) ) ;
#35390=DIRECTION ( 'NONE',  ( -0.7071067811865487940, 0.7071067811865463515, 0.000000000000000000 ) ) ;
#35391=CARTESIAN_POINT ( 'NONE',  ( -60.48921356237309510, -27.52281430457097500, 5.000000000000000000 ) ) ;
#35393=ORIENTED_EDGE ( 'NONE', *, *, #40069, .T. ) ;
#35394=EDGE_LOOP ( 'NONE', ( #47353, #101206, #42177, #20403 ) ) ;
#35395=ORIENTED_EDGE ( 'NONE', *, *, #19898, .T. ) ;
#35397=ADVANCED_FACE ( 'NONE', ( #20088 ), #64336, .F. ) ;
#35398=VECTOR ( 'NONE', #99648, 1000.000000000000000 ) ;
#35399=ORIENTED_EDGE ( 'NONE', *, *, #65602, .F. ) ;
#35400=ADVANCED_FACE ( 'NONE', ( #7783 ), #139046, .F. ) ;
#35401=CARTESIAN_POINT ( 'NONE',  ( 69.29974487139159578, -27.71228299555254537, 4.000000000000000000 ) ) ;
#35402=DIRECTION ( 'NONE',  ( 0.7071067811865487940, 0.7071067811865463515, -0.000000000000000000 ) ) ;
#35403=CARTESIAN_POINT ( 'NONE',  ( 34.49999999999975842, 16.46425560840032531, 4.994342998332160555 ) ) ;
#35404=CARTESIAN_POINT ( 'NONE',  ( -11.51078643762690490, -27.52281430457047406, 5.000000000000000000 ) ) ;
#35405=ORIENTED_EDGE ( 'NONE', *, *, #108121, .F. ) ;
#35406=EDGE_CURVE ( 'NONE', #20788, #97211, #133014, .T. ) ;
#35408=DIRECTION ( 'NONE',  ( -0.7071067811865487940, 0.7071067811865463515, -0.000000000000000000 ) ) ;
#35409=VECTOR ( 'NONE', #74674, 1000.000000000000227 ) ;
#35410=LINE ( 'NONE', #47024, #83590 ) ;
#35412=VERTEX_POINT ( 'NONE', #73780 ) ;
#35414=LINE ( 'NONE', #91885, #16509 ) ;
#35415=EDGE_CURVE ( 'NONE', #3888, #72508, #91619, .T. ) ;
#35416=CARTESIAN_POINT ( 'NONE',  ( 3.707106781186523481, 20.25929247661551713, 5.000000000000000000 ) ) ;
#35418=VECTOR ( 'NONE', #33943, 1000.000000000000000 ) ;
#35424=EDGE_CURVE ( 'NONE', #82359, #60304, #37238, .T. ) ;
#35426=CARTESIAN_POINT ( 'NONE',  ( -11.99999999999992006, 10.21212019023808004, -2.019456568337770985 ) ) ;
#35427=VECTOR ( 'NONE', #97888, 1000.000000000000227 ) ;
#35428=PLANE ( 'NONE',  #65943 ) ;
#35430=EDGE_CURVE ( 'NONE', #86472, #20317, #90178, .T. ) ;
#35431=ORIENTED_EDGE ( 'NONE', *, *, #99554, .F. ) ;
#35432=ORIENTED_EDGE ( 'NONE', *, *, #7291, .T. ) ;
#35433=DIRECTION ( 'NONE',  ( -0.000000000000000000, 0.000000000000000000, 1.000000000000000000 ) ) ;
#35434=ORIENTED_EDGE ( 'NONE', *, *, #28033, .F. ) ;
#35435=ORIENTED_EDGE ( 'NONE', *, *, #47132, .F. ) ;
#35436=VECTOR ( 'NONE', #39327, 1000.000000000000000 ) ;
#35437=AXIS2_PLACEMENT_3D ( 'NONE', #117329, #58759, #61583 ) ;
#35438=EDGE_CURVE ( 'NONE', #6466, #12348, #13316, .T. ) ;
#35439=LINE ( 'NONE', #123142, #17264 ) ;
#35440=ORIENTED_EDGE ( 'NONE', *, *, #124506, .F. ) ;
#35441=DIRECTION ( 'NONE',  ( 1.000000000000000000, 0.000000000000000000, 0.000000000000000000 ) ) ;
#35442=LINE ( 'NONE', #81064, #84207 ) ;
#35443=DIRECTION ( 'NONE',  ( -0.3543493200069163240, 4.681814790819596721E-17, -0.9351131265310288487 ) ) ;
#35444=CARTESIAN_POINT ( 'NONE',  ( -8.700255128608413102, -27.71228299555199825, 4.000000000000000000 ) ) ;
#35445=VECTOR ( 'NONE', #54832, 999.9999999999998863 ) ;
#35446=CARTESIAN_POINT ( 'NONE',  ( -23.99999999999982947, 14.96639925780211122, 5.000000000000000000 ) ) ;
#35448=DIRECTION ( 'NONE',  ( 0.3543493200069162685, -0.000000000000000000, -0.9351131265310288487 ) ) ;
#35449=ORIENTED_EDGE ( 'NONE', *, *, #127599, .T. ) ;
#35450=CARTESIAN_POINT ( 'NONE',  ( 1.499999999999987566, -4.796895815301019717, -3.611700055028677525 ) ) ;
#35451=ORIENTED_EDGE ( 'NONE', *, *, #72395, .T. ) ;
#35452=LINE ( 'NONE', #133317, #21367 ) ;
#35453=ORIENTED_EDGE ( 'NONE', *, *, #3332, .T. ) ;
#35454=FACE_OUTER_BOUND ( 'NONE', #111694, .T. ) ;
#35455=ORIENTED_EDGE ( 'NONE', *, *, #62059, .F. ) ;
#35457=ORIENTED_EDGE ( 'NONE', *, *, #93272, .T. ) ;
#35461=DIRECTION ( 'NONE',  ( 0.6830127018922180770, -0.6830127018922204085, -0.2588190451025213501 ) ) ;
#35462=ADVANCED_FACE ( 'NONE', ( #134425 ), #133706, .F. ) ;
#35463=PLANE ( 'NONE',  #92207 ) ;
#35464=LINE ( 'NONE', #123886, #99108 ) ;
#35465=DIRECTION ( 'NONE',  ( 0.7071067811865486830, -0.7071067811865464625, -0.000000000000000000 ) ) ;
#35466=AXIS2_PLACEMENT_3D ( 'NONE', #125344, #92688, #24587 ) ;
#35467=DIRECTION ( 'NONE',  ( -0.000000000000000000, 0.000000000000000000, 1.000000000000000000 ) ) ;
#35468=VECTOR ( 'NONE', #98045, 1000.000000000000114 ) ;
#35469=AXIS2_PLACEMENT_3D ( 'NONE', #103168, #79332, #25596 ) ;
#35471=VERTEX_POINT ( 'NONE', #46000 ) ;
#35473=DIRECTION ( 'NONE',  ( 0.7071067811865487940, 0.7071067811865463515, 0.000000000000000000 ) ) ;
#35474=CARTESIAN_POINT ( 'NONE',  ( 0.000000000000000000, 0.000000000000000000, 5.000000000000000000 ) ) ;
#35475=EDGE_LOOP ( 'NONE', ( #26296, #133001, #95211, #59875 ) ) ;
#35476=EDGE_LOOP ( 'NONE', ( #18647, #28386, #48076, #98387 ) ) ;
#35477=AXIS2_PLACEMENT_3D ( 'NONE', #109779, #997, #22733 ) ;
#35478=AXIS2_PLACEMENT_3D ( 'NONE', #133620, #114692, #124160 ) ;
#35481=ORIENTED_EDGE ( 'NONE', *, *, #71725, .F. ) ;
#35483=DIRECTION ( 'NONE',  ( 0.7071067811865487940, -0.7071067811865463515, 0.000000000000000000 ) ) ;
#35484=DIRECTION ( 'NONE',  ( -0.6830127018922180770, -0.6830127018922204085, -0.2588190451025213501 ) ) ;
#35485=ADVANCED_FACE ( 'NONE', ( #90929 ), #24229, .F. ) ;
#35486=CARTESIAN_POINT ( 'NONE',  ( 8.207106781186492839, 0.7592924766157086447, 5.000000000000000000 ) ) ;
#35488=DIRECTION ( 'NONE',  ( -0.7071067811865486830, -0.7071067811865464625, 0.000000000000000000 ) ) ;
#35489=VERTEX_POINT ( 'NONE', #112654 ) ;
#35490=DIRECTION ( 'NONE',  ( 0.7071067811865486830, -0.7071067811865464625, -0.000000000000000000 ) ) ;
#35491=ADVANCED_FACE ( 'NONE', ( #69912 ), #24920, .F. ) ;
#35492=EDGE_CURVE ( 'NONE', #58967, #84831, #35852, .T. ) ;
#35493=VECTOR ( 'NONE', #19780, 1000.000000000000000 ) ;
#35495=ORIENTED_EDGE ( 'NONE', *, *, #775, .T. ) ;
#35497=CARTESIAN_POINT ( 'NONE',  ( 5.292893218813420120, 14.25929247661557753, 5.000000000000000000 ) ) ;
#35498=EDGE_CURVE ( 'NONE', #29089, #139138, #2434, .T. ) ;
#35500=VERTEX_POINT ( 'NONE', #34385 ) ;
#35504=DIRECTION ( 'NONE',  ( 0.7071067811865487940, 0.7071067811865463515, 0.000000000000000000 ) ) ;
#35505=CARTESIAN_POINT ( 'NONE',  ( -32.99999999999976552, 1.931123077392167264, 4.000000000000000000 ) ) ;
#35506=CARTESIAN_POINT ( 'NONE',  ( 0.000000000000000000, 0.000000000000000000, 5.000000000000000000 ) ) ;
#35507=EDGE_LOOP ( 'NONE', ( #13244, #20762, #100338, #39378 ) ) ;
#35508=VECTOR ( 'NONE', #24378, 1000.000000000000227 ) ;
#35509=DIRECTION ( 'NONE',  ( 0.7071067811865487940, 0.7071067811865463515, -0.000000000000000000 ) ) ;
#35513=PLANE ( 'NONE',  #130216 ) ;
#35514=ORIENTED_EDGE ( 'NONE', *, *, #112612, .F. ) ;
#35515=ADVANCED_FACE ( 'NONE', ( #45295 ), #59044, .F. ) ;
#35516=CYLINDRICAL_SURFACE ( 'NONE', #63303, 0.5000000000000004441 ) ;
#35517=ORIENTED_EDGE ( 'NONE', *, *, #93089, .F. ) ;
#35518=VECTOR ( 'NONE', #56193, 1000.000000000000227 ) ;
#35520=VERTEX_POINT ( 'NONE', #78604 ) ;
#35521=EDGE_LOOP ( 'NONE', ( #34530, #99856, #58927 ) ) ;
#35523=FACE_OUTER_BOUND ( 'NONE', #37803, .T. ) ;
#35524=ADVANCED_FACE ( 'NONE', ( #5992 ), #72777, .F. ) ;
#35525=EDGE_LOOP ( 'NONE', ( #37343, #65284, #138302, #95868 ) ) ;
#35526=CARTESIAN_POINT ( 'NONE',  ( 29.99451991528749417, 28.92564299267958816, 4.000000000000000000 ) ) ;
#35527=EDGE_CURVE ( 'NONE', #30609, #93966, #35220, .T. ) ;
#35528=ORIENTED_EDGE ( 'NONE', *, *, #76881, .F. ) ;
#35529=CARTESIAN_POINT ( 'NONE',  ( 1.301042606982605321E-15, -21.03360074219752462, 5.000000000000000000 ) ) ;
#35530=CARTESIAN_POINT ( 'NONE',  ( -30.29974487139158867, -27.71228299555227537, 4.000000000000000000 ) ) ;
#35531=LINE ( 'NONE', #124635, #73960 ) ;
#35532=VECTOR ( 'NONE', #91635, 1000.000000000000000 ) ;
#35533=CARTESIAN_POINT ( 'NONE',  ( 32.99999999999977263, -10.77435723561691994, -9.972017380717304036 ) ) ;
#35534=PLANE ( 'NONE',  #2550 ) ;
#35535=DIRECTION ( 'NONE',  ( -0.000000000000000000, 1.000000000000000000, -0.000000000000000000 ) ) ;
#35536=CARTESIAN_POINT ( 'NONE',  ( -25.49999999999981526, -4.912538124160705344, 4.000000000000000000 ) ) ;
#35538=LINE ( 'NONE', #13006, #131747 ) ;
#35540=LINE ( 'NONE', #80452, #81503 ) ;
#35541=CARTESIAN_POINT ( 'NONE',  ( 0.000000000000000000, 0.000000000000000000, 5.000000000000000000 ) ) ;
#35542=FACE_OUTER_BOUND ( 'NONE', #58562, .T. ) ;
#35543=DIRECTION ( 'NONE',  ( 1.000000000000000000, 0.000000000000000000, 0.000000000000000000 ) ) ;
#35544=EDGE_LOOP ( 'NONE', ( #104207, #86017, #91465, #57168 ) ) ;
#35545=EDGE_CURVE ( 'NONE', #53228, #7053, #90271, .T. ) ;
#35546=ORIENTED_EDGE ( 'NONE', *, *, #43837, .T. ) ;
#35550=ORIENTED_EDGE ( 'NONE', *, *, #118263, .T. ) ;
#35551=EDGE_CURVE ( 'NONE', #121120, #20950, #22437, .T. ) ;
#35552=EDGE_LOOP ( 'NONE', ( #103122, #77110, #55223, #104043 ) ) ;
#35553=CARTESIAN_POINT ( 'NONE',  ( 2.999999999999980016, -15.03360074219758680, 5.000000000000000000 ) ) ;
#35557=DIRECTION ( 'NONE',  ( -0.7071067811865487940, 0.7071067811865463515, 0.000000000000000000 ) ) ;
#35558=EDGE_CURVE ( 'NONE', #22536, #54738, #77998, .T. ) ;
#35559=CARTESIAN_POINT ( 'NONE',  ( -11.51078643762690490, -27.52281430457047406, 5.000000000000000000 ) ) ;
#35560=LINE ( 'NONE', #23938, #115821 ) ;
#35562=EDGE_CURVE ( 'NONE', #109374, #26207, #79463, .T. ) ;
#35563=DIRECTION ( 'NONE',  ( 0.7071067811865487940, 0.7071067811865463515, -0.000000000000000000 ) ) ;
#35564=PLANE ( 'NONE',  #84069 ) ;
#35565=DIRECTION ( 'NONE',  ( 1.000000000000000000, 0.000000000000000000, 0.000000000000000000 ) ) ;
#35567=CARTESIAN_POINT ( 'NONE',  ( 6.183988606268994381, 28.73617430169791476, 5.000000000000000000 ) ) ;
#35570=DIRECTION ( 'NONE',  ( 0.7071067811865487940, 0.7071067811865463515, -0.000000000000000000 ) ) ;
#35573=ORIENTED_EDGE ( 'NONE', *, *, #3055, .T. ) ;
#35574=VERTEX_POINT ( 'NONE', #58426 ) ;
#35576=VECTOR ( 'NONE', #109948, 1000.000000000000000 ) ;
#35577=ORIENTED_EDGE ( 'NONE', *, *, #38789, .F. ) ;
#35581=EDGE_CURVE ( 'NONE', #86059, #66739, #25008, .T. ) ;
#35582=PLANE ( 'NONE',  #51452 ) ;
#35583=LINE ( 'NONE', #58044, #32779 ) ;
#35584=VECTOR ( 'NONE', #52180, 1000.000000000000000 ) ;
#35586=ORIENTED_EDGE ( 'NONE', *, *, #108867, .T. ) ;
#35589=AXIS2_PLACEMENT_3D ( 'NONE', #116926, #6692, #106744 ) ;
#35591=LINE ( 'NONE', #123995, #133486 ) ;
#35592=ORIENTED_EDGE ( 'NONE', *, *, #105743, .F. ) ;
#35593=ORIENTED_EDGE ( 'NONE', *, *, #70888, .T. ) ;
#35594=ORIENTED_EDGE ( 'NONE', *, *, #138766, .T. ) ;
#35595=CARTESIAN_POINT ( 'NONE',  ( -1.500000000000001332, 16.08746187583908949, 4.000000000000000000 ) ) ;
#35598=VECTOR ( 'NONE', #69856, 1000.000000000000227 ) ;
#35599=EDGE_CURVE ( 'NONE', #45797, #10935, #111304, .T. ) ;
#35602=VERTEX_POINT ( 'NONE', #45389 ) ;
#35604=CARTESIAN_POINT ( 'NONE',  ( -26.28242261357414122, -21.73023691814492508, 5.000000000000000888 ) ) ;
#35605=VERTEX_POINT ( 'NONE', #47548 ) ;
#35606=ORIENTED_EDGE ( 'NONE', *, *, #36850, .F. ) ;
#35607=ORIENTED_EDGE ( 'NONE', *, *, #75234, .T. ) ;
#35608=AXIS2_PLACEMENT_3D ( 'NONE', #132835, #13846, #47281 ) ;
#35610=CARTESIAN_POINT ( 'NONE',  ( 36.48921356237310221, -27.52281430457080802, 5.000000000000000000 ) ) ;
#35612=VERTEX_POINT ( 'NONE', #91704 ) ;
#35613=VECTOR ( 'NONE', #53084, 1000.000000000000000 ) ;
#35614=CARTESIAN_POINT ( 'NONE',  ( -30.48921356237309510, -27.52281430457076894, 5.000000000000000000 ) ) ;
#35616=FACE_BOUND ( 'NONE', #131875, .T. ) ;
#35617=ORIENTED_EDGE ( 'NONE', *, *, #17351, .T. ) ;
#35618=LINE ( 'NONE', #88555, #126690 ) ;
#35619=DIRECTION ( 'NONE',  ( 0.7071067811865486830, -0.7071067811865464625, -0.000000000000000000 ) ) ;
#35620=CARTESIAN_POINT ( 'NONE',  ( 0.000000000000000000, 0.000000000000000000, 5.000000000000000000 ) ) ;
#35621=ORIENTED_EDGE ( 'NONE', *, *, #49062, .F. ) ;
#35622=CARTESIAN_POINT ( 'NONE',  ( 27.79289321881326558, -14.24070752338414003, 5.000000000000000000 ) ) ;
#35624=ORIENTED_EDGE ( 'NONE', *, *, #16668, .T. ) ;
#35626=AXIS2_PLACEMENT_3D ( 'NONE', #94583, #84466, #82316 ) ;
#35632=ORIENTED_EDGE ( 'NONE', *, *, #83055, .F. ) ;
#35633=DIRECTION ( 'NONE',  ( 0.7071067811865486830, -0.7071067811865464625, -0.000000000000000000 ) ) ;
#35634=DIRECTION ( 'NONE',  ( -0.6830127018922180770, -0.6830127018922204085, -0.2588190451025213501 ) ) ;
#35635=VECTOR ( 'NONE', #138231, 1000.000000000000000 ) ;
#35636=( BOUNDED_CURVE ( )  B_SPLINE_CURVE ( 3, ( #37307, #80130, #45364, #136602 ),
 .UNSPECIFIED., .F., .F. ) 
 B_SPLINE_CURVE_WITH_KNOTS ( ( 4, 4 ),
 ( 5.106027341939284980, 6.645403452391244414 ),
 .UNSPECIFIED. ) 
 CURVE ( )  GEOMETRIC_REPRESENTATION_ITEM ( )  RATIONAL_B_SPLINE_CURVE ( ( 1.000000000000000000, 0.8120851936182289510, 0.8120851936182289510, 1.000000000000000000 ) ) 
 REPRESENTATION_ITEM ( '' )  );
#35638=CARTESIAN_POINT ( 'NONE',  ( 5.207106781186502609, 15.75929247661555976, 5.000000000000000000 ) ) ;
#35640=EDGE_CURVE ( 'NONE', #23427, #111757, #57690, .T. ) ;
#35641=ORIENTED_EDGE ( 'NONE', *, *, #12524, .F. ) ;
#35642=ORIENTED_EDGE ( 'NONE', *, *, #66725, .F. ) ;
#35643=ADVANCED_FACE ( 'NONE', ( #46838 ), #91025, .T. ) ;
#35644=AXIS2_PLACEMENT_3D ( 'NONE', #103891, #60452, #6699 ) ;
#35645=ORIENTED_EDGE ( 'NONE', *, *, #40173, .T. ) ;
#35646=ORIENTED_EDGE ( 'NONE', *, *, #138619, .F. ) ;
#35647=LINE ( 'NONE', #41302, #128223 ) ;
#35648=VERTEX_POINT ( 'NONE', #34482 ) ;
#35650=ORIENTED_EDGE ( 'NONE', *, *, #116467, .F. ) ;
#35651=CARTESIAN_POINT ( 'NONE',  ( -6.489213562373093325, -27.52281430457059841, 5.000000000000000000 ) ) ;
#35652=PLANE ( 'NONE',  #89619 ) ;
#35653=EDGE_CURVE ( 'NONE', #107445, #120101, #23595, .T. ) ;
#35654=EDGE_CURVE ( 'NONE', #119678, #76576, #92401, .T. ) ;
#35655=LINE ( 'NONE', #122612, #62477 ) ;
#35656=VECTOR ( 'NONE', #82624, 1000.000000000000000 ) ;
#35657=ORIENTED_EDGE ( 'NONE', *, *, #97206, .T. ) ;
#35658=FACE_OUTER_BOUND ( 'NONE', #87492, .T. ) ;
#35659=ORIENTED_EDGE ( 'NONE', *, *, #9960, .T. ) ;
#35661=EDGE_CURVE ( 'NONE', #36236, #101036, #103534, .T. ) ;
#35664=AXIS2_PLACEMENT_3D ( 'NONE', #34035, #657, #66656 ) ;
#35665=CARTESIAN_POINT ( 'NONE',  ( -9.489213562373095101, -27.52281430457062328, 5.000000000000000000 ) ) ;
#35670=CARTESIAN_POINT ( 'NONE',  ( -9.328169399223463998, 5.259292476615662792, 4.000000000000000000 ) ) ;
#35671=CARTESIAN_POINT ( 'NONE',  ( -34.49999999999975842, -7.535744391599424219, 4.994342998332167660 ) ) ;
#35672=ORIENTED_EDGE ( 'NONE', *, *, #25009, .F. ) ;
#35673=CARTESIAN_POINT ( 'NONE',  ( 63.29974487139158867, -27.71228299555250274, 4.000000000000000000 ) ) ;
#35674=FACE_OUTER_BOUND ( 'NONE', #141656, .T. ) ;
#35675=VERTEX_POINT ( 'NONE', #126461 ) ;
#35676=DIRECTION ( 'NONE',  ( 0.7071067811865487940, 0.7071067811865463515, -0.000000000000000000 ) ) ;
#35677=ORIENTED_EDGE ( 'NONE', *, *, #116409, .T. ) ;
#35678=EDGE_CURVE ( 'NONE', #52654, #31895, #3932, .T. ) ;
#35680=CARTESIAN_POINT ( 'NONE',  ( -20.99999999999985079, 12.25461709320619086, -10.07315571508702057 ) ) ;
#35681=DIRECTION ( 'NONE',  ( -0.7071067811865486830, 0.7071067811865464625, 0.000000000000000000 ) ) ;
#35683=VECTOR ( 'NONE', #1347, 1000.000000000000000 ) ;
#35684=EDGE_LOOP ( 'NONE', ( #84510, #89150, #90089, #117183 ) ) ;
#35685=DIRECTION ( 'NONE',  ( 0.7071067811865487940, 0.7071067811865463515, 0.000000000000000000 ) ) ;
#35686=EDGE_CURVE ( 'NONE', #106062, #135320, #6082, .T. ) ;
#35687=CARTESIAN_POINT ( 'NONE',  ( 1.499999999999992673, -10.53360074219763476, 5.000000000000000000 ) ) ;
#35688=CARTESIAN_POINT ( 'NONE',  ( -11.29298673570688649, -21.74070752338406720, 4.999753212805217117 ) ) ;
#35689=EDGE_LOOP ( 'NONE', ( #134119, #127009, #85151, #31022 ) ) ;
#35690=DIRECTION ( 'NONE',  ( 0.7071067811865487940, 0.7071067811865463515, 0.000000000000000000 ) ) ;
#35691=ORIENTED_EDGE ( 'NONE', *, *, #110437, .F. ) ;
#35692=EDGE_CURVE ( 'NONE', #120761, #89471, #72145, .T. ) ;
#35693=DIRECTION ( 'NONE',  ( -0.000000000000000000, 0.3543493200069153248, 0.9351131265310292928 ) ) ;
#35694=CARTESIAN_POINT ( 'NONE',  ( 30.48921356237309510, -27.52281430457076894, 5.000000000000000000 ) ) ;
#35695=ORIENTED_EDGE ( 'NONE', *, *, #8768, .T. ) ;
#35696=VERTEX_POINT ( 'NONE', #127928 ) ;
#35697=CARTESIAN_POINT ( 'NONE',  ( 34.40832548098979515, -0.7407075233842770334, 14.76736230305388631 ) ) ;
#35699=AXIS2_PLACEMENT_3D ( 'NONE', #107077, #119360, #30232 ) ;
#35700=EDGE_CURVE ( 'NONE', #77699, #27215, #39490, .T. ) ;
#35701=VERTEX_POINT ( 'NONE', #61961 ) ;
#35702=VECTOR ( 'NONE', #83496, 1000.000000000000000 ) ;
#35706=CARTESIAN_POINT ( 'NONE',  ( 62.99451991528749772, 28.92564299267982264, 4.000000000000000000 ) ) ;
#35708=EDGE_CURVE ( 'NONE', #117516, #30259, #6794, .T. ) ;
#35709=CARTESIAN_POINT ( 'NONE',  ( 66.18398860626901126, 28.73617430169833753, 5.000000000000000000 ) ) ;
#35711=LINE ( 'NONE', #137129, #76697 ) ;
#35712=EDGE_LOOP ( 'NONE', ( #56759, #132324, #71948, #86998 ) ) ;
#35713=VERTEX_POINT ( 'NONE', #28077 ) ;
#35714=ORIENTED_EDGE ( 'NONE', *, *, #60016, .F. ) ;
#35715=EDGE_CURVE ( 'NONE', #9875, #106324, #6985, .T. ) ;
#35717=ORIENTED_EDGE ( 'NONE', *, *, #33278, .F. ) ;
#35719=ORIENTED_EDGE ( 'NONE', *, *, #91957, .F. ) ;
#35720=EDGE_CURVE ( 'NONE', #134437, #97146, #124189, .T. ) ;
#35723=CARTESIAN_POINT ( 'NONE',  ( -32.67183060077623935, 17.25929247661554200, 4.000000000000000000 ) ) ;
#35724=VERTEX_POINT ( 'NONE', #69114 ) ;
#35727=VECTOR ( 'NONE', #112499, 1000.000000000000000 ) ;
#35728=EDGE_CURVE ( 'NONE', #128989, #57042, #90873, .T. ) ;
#35729=CARTESIAN_POINT ( 'NONE',  ( 27.42327845806336839, 11.25929247661559884, 17.85071094206578124 ) ) ;
#35730=VECTOR ( 'NONE', #54550, 999.9999999999998863 ) ;
#35733=ORIENTED_EDGE ( 'NONE', *, *, #105834, .T. ) ;
#35734=FACE_OUTER_BOUND ( 'NONE', #83806, .T. ) ;
#35735=LINE ( 'NONE', #1593, #33430 ) ;
#35737=DIRECTION ( 'NONE',  ( 0.7071067811865487940, -0.7071067811865463515, 0.000000000000000000 ) ) ;
#35738=CARTESIAN_POINT ( 'NONE',  ( 2.510786437626908008, -27.52281430457053446, 5.000000000000000000 ) ) ;
#35740=VECTOR ( 'NONE', #18817, 1000.000000000000000 ) ;
#35742=DIRECTION ( 'NONE',  ( 0.7071067811865487940, 0.7071067811865463515, -0.000000000000000000 ) ) ;
#35743=VECTOR ( 'NONE', #28514, 999.9999999999998863 ) ;
#35744=DIRECTION ( 'NONE',  ( 0.7071067811865487940, -0.7071067811865463515, 0.000000000000000000 ) ) ;
#35745=EDGE_LOOP ( 'NONE', ( #7300, #25959, #114475, #70058, #7914, #88003, #22303, #119946, #34850, #109401, #136926, #19626, #126465, #31491, #3099, #109093, #92620, #132456, #13764, #66176, #67552, #84111, #113819, #80536, #68055, #70923, #134881, #118904, #136632, #51469, #117353, #52646, #29489, #59539, #83054, #49191, #141123, #37999, #14191, #102061, #91043, #37053, #103156, #75553, #30361, #83825, #117265, #108274, #65525, #115205, #91777, #141927, #37276, #140911, #97274, #86211, #13802, #105251, #2967, #2176, #75019, #110141, #15942, #54045, #102149, #39525, #142490, #32889, #9214, #17376, #111427, #64006, #23820, #30808, #61050, #54222, #104518, #76237, #101378, #116878, #106935, #79916, #87697, #121651, #8398, #77830, #86636, #97913, #71133, #80323, #99591, #39135, #141498, #99096, #42460, #22678, #98141, #134624, #141506, #121922, #72086, #50850, #42922, #72220, #85646 ) ) ;
#35746=ORIENTED_EDGE ( 'NONE', *, *, #91681, .T. ) ;
#35748=VERTEX_POINT ( 'NONE', #110432 ) ;
#35749=EDGE_CURVE ( 'NONE', #22223, #78390, #228, .T. ) ;
#35750=DIRECTION ( 'NONE',  ( -0.000000000000000000, 0.3543493200069152138, -0.9351131265310292928 ) ) ;
#35751=EDGE_LOOP ( 'NONE', ( #2793, #88351, #111578, #409 ) ) ;
#35752=CARTESIAN_POINT ( 'NONE',  ( -30.79289321881324071, -11.24070752338416668, 5.000000000000000000 ) ) ;
#35753=DIRECTION ( 'NONE',  ( -0.000000000000000000, 0.000000000000000000, 1.000000000000000000 ) ) ;
#35755=ADVANCED_FACE ( 'NONE', ( #49522 ), #114024, .F. ) ;
#35756=VERTEX_POINT ( 'NONE', #3787 ) ;
#35757=CARTESIAN_POINT ( 'NONE',  ( 27.70710678118635428, 5.259292476615659240, 5.000000000000000000 ) ) ;
#35758=VERTEX_POINT ( 'NONE', #6638 ) ;
#35759=AXIS2_PLACEMENT_3D ( 'NONE', #19051, #63313, #111591 ) ;
#35760=DIRECTION ( 'NONE',  ( 0.7071067811865486830, -0.7071067811865464625, -0.000000000000000000 ) ) ;
#35761=CARTESIAN_POINT ( 'NONE',  ( 2.999999999999975131, -22.06887692260758982, 4.000000000000000000 ) ) ;
#35762=LINE ( 'NONE', #65531, #83719 ) ;
#35765=EDGE_CURVE ( 'NONE', #115630, #132022, #50643, .T. ) ;
#35766=CARTESIAN_POINT ( 'NONE',  ( 2.510786437626908008, -27.52281430457053446, 5.000000000000000000 ) ) ;
#35767=VERTEX_POINT ( 'NONE', #59672 ) ;
#35769=DIRECTION ( 'NONE',  ( 0.000000000000000000, 0.3543493200069153248, 0.9351131265310291818 ) ) ;
#35770=CARTESIAN_POINT ( 'NONE',  ( -16.06996025486399304, -0.7407075233842735917, 13.87443053587614905 ) ) ;
#35771=CARTESIAN_POINT ( 'NONE',  ( -15.48921356237309510, -27.52281430457066236, 5.000000000000000000 ) ) ;
#35772=LINE ( 'NONE', #80679, #29950 ) ;
#35773=CARTESIAN_POINT ( 'NONE',  ( -6.299744871391586898, -27.71228299555210484, 4.000000000000000000 ) ) ;
#35775=CARTESIAN_POINT ( 'NONE',  ( -0.3281693992235306667, 8.259292476615636147, 4.000000000000000000 ) ) ;
#35776=DIRECTION ( 'NONE',  ( -0.7071067811865486830, -0.7071067811865464625, -0.000000000000000000 ) ) ;
#35777=CARTESIAN_POINT ( 'NONE',  ( 5.999999999999960032, -1.068876922607809421, 4.000000000000000000 ) ) ;
#35778=ORIENTED_EDGE ( 'NONE', *, *, #22089, .T. ) ;
#35780=CARTESIAN_POINT ( 'NONE',  ( 11.84387692260750136, -22.22500000000000497, 4.000000000000000000 ) ) ;
#35781=ORIENTED_EDGE ( 'NONE', *, *, #85963, .T. ) ;
#35782=AXIS2_PLACEMENT_3D ( 'NONE', #42209, #141505, #89263 ) ;
#35783=ADVANCED_FACE ( 'NONE', ( #115407 ), #105970, .F. ) ;
#35784=EDGE_CURVE ( 'NONE', #125467, #93695, #80707, .T. ) ;
#35785=FACE_OUTER_BOUND ( 'NONE', #8485, .T. ) ;
#35786=ORIENTED_EDGE ( 'NONE', *, *, #139898, .T. ) ;
#35787=DIRECTION ( 'NONE',  ( -0.000000000000000000, 0.000000000000000000, 1.000000000000000000 ) ) ;
#35788=FACE_BOUND ( 'NONE', #127693, .T. ) ;
#35789=EDGE_CURVE ( 'NONE', #137119, #88854, #105283, .T. ) ;
#35790=CARTESIAN_POINT ( 'NONE',  ( 81.18398860626899705, 28.73617430169844056, 5.000000000000000000 ) ) ;
#35791=LINE ( 'NONE', #133649, #76762 ) ;
#35792=DIRECTION ( 'NONE',  ( 0.7071067811865487940, 0.7071067811865463515, 0.000000000000000000 ) ) ;
#35793=CARTESIAN_POINT ( 'NONE',  ( 12.29974487139158512, -27.71228299555214747, 4.000000000000000000 ) ) ;
#35794=ORIENTED_EDGE ( 'NONE', *, *, #43640, .T. ) ;
#35795=VECTOR ( 'NONE', #132817, 999.9999999999998863 ) ;
#35797=LINE ( 'NONE', #126329, #85672 ) ;
#35800=ORIENTED_EDGE ( 'NONE', *, *, #56704, .T. ) ;
#35802=VERTEX_POINT ( 'NONE', #92252 ) ;
#35804=LINE ( 'NONE', #59002, #39732 ) ;
#35805=VECTOR ( 'NONE', #133754, 999.9999999999998863 ) ;
#35806=ORIENTED_EDGE ( 'NONE', *, *, #76899, .T. ) ;
#35807=DIRECTION ( 'NONE',  ( 0.7071067811865487940, -0.7071067811865463515, 0.000000000000000000 ) ) ;
#35808=CARTESIAN_POINT ( 'NONE',  ( -33.18398860626899705, 28.73617430169810305, 5.000000000000000000 ) ) ;
#35809=PLANE ( 'NONE',  #22262 ) ;
#35810=VECTOR ( 'NONE', #29562, 1000.000000000000000 ) ;
#35811=LINE ( 'NONE', #59012, #106009 ) ;
#35812=FACE_OUTER_BOUND ( 'NONE', #11571, .T. ) ;
#35813=DIRECTION ( 'NONE',  ( -0.3543493200069162685, -0.000000000000000000, -0.9351131265310288487 ) ) ;
#35814=DIRECTION ( 'NONE',  ( 0.7071067811865487940, 0.7071067811865463515, 0.000000000000000000 ) ) ;
#35815=ORIENTED_EDGE ( 'NONE', *, *, #131562, .T. ) ;
#35816=VERTEX_POINT ( 'NONE', #26312 ) ;
#35817=DIRECTION ( 'NONE',  ( -0.7071067811865487940, 0.7071067811865463515, 0.000000000000000000 ) ) ;
#35819=ORIENTED_EDGE ( 'NONE', *, *, #113382, .T. ) ;
#35820=ORIENTED_EDGE ( 'NONE', *, *, #7677, .F. ) ;
#35821=ORIENTED_EDGE ( 'NONE', *, *, #81920, .F. ) ;
#35822=EDGE_CURVE ( 'NONE', #97476, #9196, #5236, .T. ) ;
#35824=VERTEX_POINT ( 'NONE', #137932 ) ;
#35825=DIRECTION ( 'NONE',  ( -0.7071067811865486830, -0.7071067811865464625, -0.000000000000000000 ) ) ;
#35827=AXIS2_PLACEMENT_3D ( 'NONE', #80934, #124419, #36010 ) ;
#35829=EDGE_CURVE ( 'NONE', #32049, #102811, #65505, .T. ) ;
#35830=EDGE_CURVE ( 'NONE', #83534, #10814, #82843, .T. ) ;
#35833=AXIS2_PLACEMENT_3D ( 'NONE', #131577, #54742, #128196 ) ;
#35834=LINE ( 'NONE', #80055, #139866 ) ;
#35835=EDGE_CURVE ( 'NONE', #110472, #61053, #139388, .T. ) ;
#35836=ORIENTED_EDGE ( 'NONE', *, *, #96654, .T. ) ;
#35837=AXIS2_PLACEMENT_3D ( 'NONE', #125261, #33981, #114379 ) ;
#35838=CARTESIAN_POINT ( 'NONE',  ( -34.92500000000001137, 21.72500000000000142, 5.000000000000000000 ) ) ;
#35839=ADVANCED_FACE ( 'NONE', ( #25575 ), #28461, .F. ) ;
#35840=DIRECTION ( 'NONE',  ( -0.7071067811865486830, -0.7071067811865464625, 0.000000000000000000 ) ) ;
#35841=FACE_OUTER_BOUND ( 'NONE', #26744, .T. ) ;
#35842=LINE ( 'NONE', #133696, #51829 ) ;
#35843=EDGE_LOOP ( 'NONE', ( #107781, #141760, #108185, #83098 ) ) ;
#35844=ORIENTED_EDGE ( 'NONE', *, *, #79594, .T. ) ;
#35845=EDGE_CURVE ( 'NONE', #63680, #126408, #69850, .T. ) ;
#35846=CARTESIAN_POINT ( 'NONE',  ( 3.183988606268992161, 28.73617430169789699, 5.000000000000000000 ) ) ;
#35847=CARTESIAN_POINT ( 'NONE',  ( 24.70701326429286482, -21.74070752338406365, 4.999753212805220670 ) ) ;
#35848=PLANE ( 'NONE',  #123571 ) ;
#35850=VECTOR ( 'NONE', #46136, 1000.000000000000000 ) ;
#35851=DIRECTION ( 'NONE',  ( -0.7071067811865486830, -0.7071067811865464625, 0.000000000000000000 ) ) ;
#35852=LINE ( 'NONE', #14035, #71127 ) ;
#35853=ADVANCED_FACE ( 'NONE', ( #17548 ), #48071, .F. ) ;
#35854=CARTESIAN_POINT ( 'NONE',  ( -24.70679250724059628, 20.25929247661551358, 20.83292124670820655 ) ) ;
#35856=PLANE ( 'NONE',  #116622 ) ;
#35857=ORIENTED_EDGE ( 'NONE', *, *, #90330, .F. ) ;
#35859=CARTESIAN_POINT ( 'NONE',  ( 78.48921356237309510, -27.52281430457109934, 5.000000000000000000 ) ) ;
#35862=CARTESIAN_POINT ( 'NONE',  ( 71.99451991528749772, 28.92564299267988304, 4.000000000000000000 ) ) ;
#35863=LINE ( 'NONE', #56896, #80754 ) ;
#35864=EDGE_CURVE ( 'NONE', #48713, #4046, #42912, .T. ) ;
#35865=ORIENTED_EDGE ( 'NONE', *, *, #11759, .T. ) ;
#35866=ORIENTED_EDGE ( 'NONE', *, *, #90268, .T. ) ;
#35868=DIRECTION ( 'NONE',  ( -0.3543493200069163795, -9.265275131829747941E-33, -0.9351131265310288487 ) ) ;
#35870=DIRECTION ( 'NONE',  ( 0.000000000000000000, -1.000000000000000000, 0.000000000000000000 ) ) ;
#35871=CARTESIAN_POINT ( 'NONE',  ( -39.18398860626899705, 28.73617430169814568, 5.000000000000000000 ) ) ;
#35872=CARTESIAN_POINT ( 'NONE',  ( 13.11151487241214930, 3.778085383357085547, 4.109577000315250750 ) ) ;
#35874=FACE_OUTER_BOUND ( 'NONE', #73600, .T. ) ;
#35876=DIRECTION ( 'NONE',  ( -0.7071067811865486830, -0.7071067811865464625, 0.000000000000000000 ) ) ;
#35879=DIRECTION ( 'NONE',  ( 0.7071067811865487940, 0.7071067811865463515, 0.000000000000000000 ) ) ;
#35880=PLANE ( 'NONE',  #76612 ) ;
#35881=CARTESIAN_POINT ( 'NONE',  ( -44.99451991528749772, 28.92564299267969474, 4.000000000000000000 ) ) ;
#35882=EDGE_LOOP ( 'NONE', ( #127178, #126353, #62015, #44145 ) ) ;
#35883=ADVANCED_FACE ( 'NONE', ( #131326 ), #21126, .F. ) ;
#35884=EDGE_LOOP ( 'NONE', ( #42072, #31736, #41738, #57694 ) ) ;
#35887=DIRECTION ( 'NONE',  ( 0.6830127018922181881, 0.6830127018922202975, -0.2588190451025214056 ) ) ;
#35888=LINE ( 'NONE', #38017, #18499 ) ;
#35889=LINE ( 'NONE', #99667, #53320 ) ;
#35890=CARTESIAN_POINT ( 'NONE',  ( 26.28242261357414122, -21.73023691814492864, 5.000000000000000888 ) ) ;
#35891=ORIENTED_EDGE ( 'NONE', *, *, #38594, .F. ) ;
#35892=VERTEX_POINT ( 'NONE', #119696 ) ;
#35893=CARTESIAN_POINT ( 'NONE',  ( -27.70710678118634718, -3.740707523384238176, 5.000000000000000000 ) ) ;
#35894=CARTESIAN_POINT ( 'NONE',  ( -8.149948714589710264, -8.240707523384200428, 17.25253755692237334 ) ) ;
#35897=ADVANCED_FACE ( 'NONE', ( #84964 ), #32009, .F. ) ;
#35900=DIRECTION ( 'NONE',  ( 0.7071067811865487940, 0.7071067811865463515, 0.000000000000000000 ) ) ;
#35902=FACE_OUTER_BOUND ( 'NONE', #79164, .T. ) ;
#35903=ORIENTED_EDGE ( 'NONE', *, *, #48628, .T. ) ;
#35905=DIRECTION ( 'NONE',  ( 0.7071067811865486830, -0.7071067811865464625, -0.000000000000000000 ) ) ;
#35906=EDGE_CURVE ( 'NONE', #121857, #55125, #134209, .T. ) ;
#35907=CARTESIAN_POINT ( 'NONE',  ( -34.92500000000001137, 21.72500000000000142, 5.000000000000000000 ) ) ;
#35908=CARTESIAN_POINT ( 'NONE',  ( -69.29974487139159578, -27.71228299555254537, 4.000000000000000000 ) ) ;
#35909=VERTEX_POINT ( 'NONE', #75526 ) ;
#35910=CARTESIAN_POINT ( 'NONE',  ( -11.99999999999990763, -12.03360074219761700, 5.000000000000000000 ) ) ;
#35911=VECTOR ( 'NONE', #106225, 1000.000000000000000 ) ;
#35912=EDGE_CURVE ( 'NONE', #18521, #25422, #142227, .T. ) ;
#35913=DIRECTION ( 'NONE',  ( 0.7071067811865487940, 0.7071067811865463515, 0.000000000000000000 ) ) ;
#35915=PLANE ( 'NONE',  #46053 ) ;
#35916=ORIENTED_EDGE ( 'NONE', *, *, #47562, .F. ) ;
#35917=VERTEX_POINT ( 'NONE', #76240 ) ;
#35918=LINE ( 'NONE', #112729, #132359 ) ;
#35919=DIRECTION ( 'NONE',  ( -0.6830127018922181881, 0.6830127018922202975, -0.2588190451025214056 ) ) ;
#35920=EDGE_CURVE ( 'NONE', #7608, #16626, #51641, .T. ) ;
#35921=CARTESIAN_POINT ( 'NONE',  ( 12.87729808236044704, 22.22500000000000142, -13.11407768714525623 ) ) ;
#35923=ORIENTED_EDGE ( 'NONE', *, *, #87489, .T. ) ;
#35924=PLANE ( 'NONE',  #36820 ) ;
#35926=CARTESIAN_POINT ( 'NONE',  ( 9.707106781186478628, -3.740707523384246613, 5.000000000000000000 ) ) ;
#35927=CARTESIAN_POINT ( 'NONE',  ( 15.29974487139158867, -27.71228299555216879, 4.000000000000000000 ) ) ;
#35928=ORIENTED_EDGE ( 'NONE', *, *, #66847, .F. ) ;
#35929=VECTOR ( 'NONE', #96115, 1000.000000000000227 ) ;
#35930=VERTEX_POINT ( 'NONE', #107426 ) ;
#35932=AXIS2_PLACEMENT_3D ( 'NONE', #42423, #18460, #76472 ) ;
#35933=EDGE_LOOP ( 'NONE', ( #18087, #9704, #67844, #57403 ) ) ;
#35935=CARTESIAN_POINT ( 'NONE',  ( 2.700255128608413990, -27.71228299555204089, 4.000000000000000000 ) ) ;
#35936=DIRECTION ( 'NONE',  ( 0.7071067811865487940, 0.7071067811865463515, -0.000000000000000000 ) ) ;
#35937=FACE_OUTER_BOUND ( 'NONE', #76963, .T. ) ;
#35939=ORIENTED_EDGE ( 'NONE', *, *, #111919, .F. ) ;
#35940=VERTEX_POINT ( 'NONE', #64643 ) ;
#35941=PLANE ( 'NONE',  #93141 ) ;
#35943=EDGE_CURVE ( 'NONE', #3467, #91787, #18994, .T. ) ;
#35945=ADVANCED_FACE ( 'NONE', ( #8772 ), #53030, .F. ) ;
#35947=VERTEX_POINT ( 'NONE', #95835 ) ;
#35949=LINE ( 'NONE', #89576, #123507 ) ;
#35951=FACE_BOUND ( 'NONE', #21652, .T. ) ;
#35952=EDGE_CURVE ( 'NONE', #115605, #12661, #8087, .T. ) ;
#35953=DIRECTION ( 'NONE',  ( -0.7071067811865486830, -0.7071067811865464625, 0.000000000000000000 ) ) ;
#35954=LINE ( 'NONE', #133124, #136959 ) ;
#35955=PLANE ( 'NONE',  #59891 ) ;
#35959=EDGE_LOOP ( 'NONE', ( #101464, #18624, #126711, #98620 ) ) ;
#35960=ORIENTED_EDGE ( 'NONE', *, *, #81166, .T. ) ;
#35963=DIRECTION ( 'NONE',  ( -0.7071067811865487940, 0.7071067811865463515, -0.000000000000000000 ) ) ;
#35966=CARTESIAN_POINT ( 'NONE',  ( -30.29974487139158867, -27.71228299555227537, 4.000000000000000000 ) ) ;
#35968=ORIENTED_EDGE ( 'NONE', *, *, #13378, .F. ) ;
#35970=CARTESIAN_POINT ( 'NONE',  ( 15.81349135397628558, -15.74070752338412760, 8.904080028138903202 ) ) ;
#35971=FACE_OUTER_BOUND ( 'NONE', #71458, .T. ) ;
#35972=DIRECTION ( 'NONE',  ( -0.6830127018922180770, -0.6830127018922204085, -0.2588190451025213501 ) ) ;
#35973=DIRECTION ( 'NONE',  ( -0.7071067811865486830, 0.7071067811865464625, 0.000000000000000000 ) ) ;
#35974=CARTESIAN_POINT ( 'NONE',  ( -48.48921356237309510, -27.52281430457089328, 5.000000000000000000 ) ) ;
#35975=ORIENTED_EDGE ( 'NONE', *, *, #122883, .T. ) ;
#35976=CARTESIAN_POINT ( 'NONE',  ( 2.999999999999978240, 13.55218569542903140, 5.000000000000000000 ) ) ;
#35977=DIRECTION ( 'NONE',  ( 0.6830127018922181881, 0.6830127018922202975, -0.2588190451025214056 ) ) ;
#35979=EDGE_LOOP ( 'NONE', ( #8082, #81981, #98121, #55749 ) ) ;
#35980=ORIENTED_EDGE ( 'NONE', *, *, #98675, .F. ) ;
#35982=ORIENTED_EDGE ( 'NONE', *, *, #77504, .T. ) ;
#35983=VECTOR ( 'NONE', #67102, 1000.000000000000000 ) ;
#35987=DIRECTION ( 'NONE',  ( -0.6830127018922181881, 0.6830127018922202975, -0.2588190451025214056 ) ) ;
#35988=ORIENTED_EDGE ( 'NONE', *, *, #93125, .F. ) ;
#35989=EDGE_CURVE ( 'NONE', #81079, #108304, #129896, .T. ) ;
#35991=CARTESIAN_POINT ( 'NONE',  ( 11.99999999999992539, -1.447814304570815169, 5.000000000000000000 ) ) ;
#35992=ADVANCED_FACE ( 'NONE', ( #67526 ), #89252, .F. ) ;
#35993=ORIENTED_EDGE ( 'NONE', *, *, #113178, .T. ) ;
#35994=CARTESIAN_POINT ( 'NONE',  ( 60.48921356237309510, -27.52281430457097500, 5.000000000000000000 ) ) ;
#35995=DIRECTION ( 'NONE',  ( 0.7071067811865487940, 0.7071067811865463515, -0.000000000000000000 ) ) ;
#35996=EDGE_LOOP ( 'NONE', ( #109353, #40639, #58348, #35916 ) ) ;
#35997=ADVANCED_FACE ( 'NONE', ( #68256 ), #23250, .T. ) ;
#35998=DIRECTION ( 'NONE',  ( 0.7071067811865487940, 0.7071067811865463515, 0.000000000000000000 ) ) ;
#35999=LINE ( 'NONE', #114244, #96924 ) ;
#36001=ORIENTED_EDGE ( 'NONE', *, *, #34001, .T. ) ;
#36002=DIRECTION ( 'NONE',  ( -0.6830127018922180770, -0.6830127018922204085, -0.2588190451025214056 ) ) ;
#36003=VECTOR ( 'NONE', #2095, 1000.000000000000227 ) ;
#36004=ORIENTED_EDGE ( 'NONE', *, *, #47644, .T. ) ;
#36005=ORIENTED_EDGE ( 'NONE', *, *, #77932, .F. ) ;
#36006=ORIENTED_EDGE ( 'NONE', *, *, #42917, .F. ) ;
#36007=DIRECTION ( 'NONE',  ( -0.7071067811865487940, 0.7071067811865463515, -0.000000000000000000 ) ) ;
#36008=PLANE ( 'NONE',  #116289 ) ;
#36009=ADVANCED_FACE ( 'NONE', ( #10934 ), #45776, .F. ) ;
#36010=DIRECTION ( 'NONE',  ( -0.7071067811865486830, 0.7071067811865464625, 0.000000000000000000 ) ) ;
#36011=DIRECTION ( 'NONE',  ( 0.7071067811865486830, -0.7071067811865464625, -0.000000000000000000 ) ) ;
#36012=EDGE_CURVE ( 'NONE', #8053, #645, #2191, .T. ) ;
#36013=CARTESIAN_POINT ( 'NONE',  ( 1.499999999999987566, -1.592773361805372545, -6.492772025301233541 ) ) ;
#36015=DIRECTION ( 'NONE',  ( -0.000000000000000000, -0.3543493200069152693, 0.9351131265310292928 ) ) ;
#36016=ADVANCED_FACE ( 'NONE', ( #99376 ), #34890, .F. ) ;
#36017=AXIS2_PLACEMENT_3D ( 'NONE', #31086, #109340, #18736 ) ;
#36019=LINE ( 'NONE', #80240, #141190 ) ;
#36020=VECTOR ( 'NONE', #135569, 1000.000000000000000 ) ;
#36021=LINE ( 'NONE', #1197, #73850 ) ;
#36022=VECTOR ( 'NONE', #42383, 1000.000000000000000 ) ;
#36023=CARTESIAN_POINT ( 'NONE',  ( -9.299744871391588674, -27.71228299555212971, 4.000000000000000000 ) ) ;
#36024=ORIENTED_EDGE ( 'NONE', *, *, #109016, .F. ) ;
#36025=EDGE_LOOP ( 'NONE', ( #88606, #40614, #16312, #51333 ) ) ;
#36027=LINE ( 'NONE', #135342, #27830 ) ;
#36028=CARTESIAN_POINT ( 'NONE',  ( 30.48921356237309510, -27.52281430457076894, 5.000000000000000000 ) ) ;
#36030=EDGE_CURVE ( 'NONE', #92661, #133264, #46513, .T. ) ;
#36031=VECTOR ( 'NONE', #119271, 1000.000000000000000 ) ;
#36032=CARTESIAN_POINT ( 'NONE',  ( 21.29974487139158512, -27.71228299555221142, 4.000000000000000000 ) ) ;
#36033=CARTESIAN_POINT ( 'NONE',  ( -6.183988606268994381, 28.73617430169791476, 5.000000000000000000 ) ) ;
#36035=DIRECTION ( 'NONE',  ( -0.7071067811865487940, 0.7071067811865463515, -0.000000000000000000 ) ) ;
#36036=DIRECTION ( 'NONE',  ( 0.7071067811865487940, 0.7071067811865463515, 0.000000000000000000 ) ) ;
#36037=DIRECTION ( 'NONE',  ( -0.7071067811865487940, 0.7071067811865463515, -0.000000000000000000 ) ) ;
#36039=LINE ( 'NONE', #2649, #16397 ) ;
#36040=EDGE_CURVE ( 'NONE', #18692, #143444, #142912, .T. ) ;
#36043=VERTEX_POINT ( 'NONE', #100834 ) ;
#36044=CARTESIAN_POINT ( 'NONE',  ( 54.18398860626899705, 28.73617430169825226, 5.000000000000000000 ) ) ;
#36045=CARTESIAN_POINT ( 'NONE',  ( 2.483345613589531542, 22.22500000000000142, 4.500000000000000888 ) ) ;
#36046=EDGE_LOOP ( 'NONE', ( #52525, #136401, #57907, #11515 ) ) ;
#36048=CARTESIAN_POINT ( 'NONE',  ( 26.21837311707487572, 21.74787736706806740, 4.999607392498048419 ) ) ;
#36049=ORIENTED_EDGE ( 'NONE', *, *, #9807, .F. ) ;
#36050=CARTESIAN_POINT ( 'NONE',  ( 3.799968779831609744, 8.259292476615627265, 16.85664084051840206 ) ) ;
#36051=ORIENTED_EDGE ( 'NONE', *, *, #126864, .F. ) ;
#36052=CARTESIAN_POINT ( 'NONE',  ( 45.29974487139158867, -27.71228299555237840, 4.000000000000000000 ) ) ;
#36053=ORIENTED_EDGE ( 'NONE', *, *, #99117, .T. ) ;
#36055=EDGE_CURVE ( 'NONE', #137381, #62440, #110965, .T. ) ;
#36057=CARTESIAN_POINT ( 'NONE',  ( 29.29289321881324781, 20.25929247661551713, 5.000000000000000000 ) ) ;
#36058=ORIENTED_EDGE ( 'NONE', *, *, #24463, .T. ) ;
#36059=FACE_OUTER_BOUND ( 'NONE', #105938, .T. ) ;
#36060=PLANE ( 'NONE',  #91257 ) ;
#36061=CARTESIAN_POINT ( 'NONE',  ( 9.299744871391588674, -27.71228299555212971, 4.000000000000000000 ) ) ;
#36063=DIRECTION ( 'NONE',  ( 0.7071067811865486830, -0.7071067811865464625, -0.000000000000000000 ) ) ;
#36064=CARTESIAN_POINT ( 'NONE',  ( -60.48921356237309510, -27.52281430457097500, 5.000000000000000000 ) ) ;
#36065=DIRECTION ( 'NONE',  ( 0.7071067811865487940, 0.7071067811865463515, 0.000000000000000000 ) ) ;
#36067=FACE_OUTER_BOUND ( 'NONE', #136843, .T. ) ;
#36068=VERTEX_POINT ( 'NONE', #121148 ) ;
#36069=EDGE_CURVE ( 'NONE', #123911, #626, #78382, .T. ) ;
#36071=DIRECTION ( 'NONE',  ( -0.7071067811865486830, 0.7071067811865464625, 0.000000000000000000 ) ) ;
#36072=DIRECTION ( 'NONE',  ( -0.000000000000000000, -0.3543493200069152693, 0.9351131265310292928 ) ) ;
#36073=PLANE ( 'NONE',  #30806 ) ;
#36074=CARTESIAN_POINT ( 'NONE',  ( -6.183988606268994381, 28.73617430169791476, 5.000000000000000000 ) ) ;
#36076=CARTESIAN_POINT ( 'NONE',  ( -21.18398860626899349, 28.73617430169802134, 5.000000000000000000 ) ) ;
#36077=( BOUNDED_CURVE ( )  B_SPLINE_CURVE ( 3, ( #7279, #129077, #30503, #42817 ),
 .UNSPECIFIED., .F., .T. ) 
 B_SPLINE_CURVE_WITH_KNOTS ( ( 4, 4 ),
 ( 5.005968288816727174, 5.074607125596342527 ),
 .UNSPECIFIED. ) 
 CURVE ( )  GEOMETRIC_REPRESENTATION_ITEM ( )  RATIONAL_B_SPLINE_CURVE ( ( 1.000000000000000000, 0.9996074310407763175, 0.9996074310407763175, 1.000000000000000000 ) ) 
 REPRESENTATION_ITEM ( '' )  );
#36078=CARTESIAN_POINT ( 'NONE',  ( -22.49999999999984723, 16.18958161055400069, -11.56426086740816217 ) ) ;
#36079=ORIENTED_EDGE ( 'NONE', *, *, #9422, .T. ) ;
#36080=LINE ( 'NONE', #25168, #23030 ) ;
#36081=ADVANCED_FACE ( 'NONE', ( #1489 ), #110257, .F. ) ;
#36082=CARTESIAN_POINT ( 'NONE',  ( 29.99451991528749417, 28.92564299267958816, 4.000000000000000000 ) ) ;
#36083=LINE ( 'NONE', #38215, #17334 ) ;
#36084=VERTEX_POINT ( 'NONE', #121845 ) ;
#36085=CARTESIAN_POINT ( 'NONE',  ( 32.67183060077624646, -21.74070752338406010, 4.000000000000000000 ) ) ;
#36086=DIRECTION ( 'NONE',  ( -0.000000000000000000, 0.000000000000000000, 1.000000000000000000 ) ) ;
#36087=LINE ( 'NONE', #124500, #47073 ) ;
#36088=CARTESIAN_POINT ( 'NONE',  ( -27.79289321881326558, -2.240707523384257716, 5.000000000000000000 ) ) ;
#36090=ORIENTED_EDGE ( 'NONE', *, *, #25926, .T. ) ;
#36092=ORIENTED_EDGE ( 'NONE', *, *, #57189, .F. ) ;
#36093=ORIENTED_EDGE ( 'NONE', *, *, #68249, .T. ) ;
#36097=LINE ( 'NONE', #36776, #23140 ) ;
#36098=EDGE_CURVE ( 'NONE', #106128, #75266, #784, .T. ) ;
#36101=PLANE ( 'NONE',  #75520 ) ;
#36102=ORIENTED_EDGE ( 'NONE', *, *, #56927, .T. ) ;
#36103=LINE ( 'NONE', #12175, #123000 ) ;
#36104=LINE ( 'NONE', #3427, #127551 ) ;
#36106=VERTEX_POINT ( 'NONE', #123332 ) ;
#36107=EDGE_CURVE ( 'NONE', #140203, #42790, #52091, .T. ) ;
#36108=DIRECTION ( 'NONE',  ( -0.6830127018922180770, -0.6830127018922204085, -0.2588190451025213501 ) ) ;
#36109=LINE ( 'NONE', #81772, #19161 ) ;
#36110=ORIENTED_EDGE ( 'NONE', *, *, #33602, .T. ) ;
#36111=ORIENTED_EDGE ( 'NONE', *, *, #73514, .T. ) ;
#36112=EDGE_CURVE ( 'NONE', #113088, #15312, #75990, .T. ) ;
#36113=DIRECTION ( 'NONE',  ( -0.000000000000000000, -0.3543493200069152693, 0.9351131265310292928 ) ) ;
#36114=EDGE_CURVE ( 'NONE', #90068, #108003, #42672, .T. ) ;
#36115=CARTESIAN_POINT ( 'NONE',  ( 28.49999999999980815, 12.43112307739205669, 4.000000000000000000 ) ) ;
#36117=CARTESIAN_POINT ( 'NONE',  ( 6.299744871391586898, -27.71228299555210484, 4.000000000000000000 ) ) ;
#36120=LINE ( 'NONE', #80345, #20966 ) ;
#36121=FACE_OUTER_BOUND ( 'NONE', #61391, .T. ) ;
#36122=VECTOR ( 'NONE', #100265, 1000.000000000000000 ) ;
#36123=ORIENTED_EDGE ( 'NONE', *, *, #25908, .F. ) ;
#36124=AXIS2_PLACEMENT_3D ( 'NONE', #107992, #111588, #12267 ) ;
#36126=VECTOR ( 'NONE', #120346, 1000.000000000000000 ) ;
#36128=ORIENTED_EDGE ( 'NONE', *, *, #72165, .F. ) ;
#36129=ORIENTED_EDGE ( 'NONE', *, *, #23139, .F. ) ;
#36131=DIRECTION ( 'NONE',  ( -0.000000000000000000, -0.3543493200069152693, 0.9351131265310292928 ) ) ;
#36133=DIRECTION ( 'NONE',  ( -0.7071067811865487940, 0.7071067811865463515, -0.000000000000000000 ) ) ;
#36135=DIRECTION ( 'NONE',  ( -0.000000000000000000, 0.3543493200069153248, 0.9351131265310292928 ) ) ;
#36136=CARTESIAN_POINT ( 'NONE',  ( 54.48921356237310221, -27.52281430457093236, 5.000000000000000000 ) ) ;
#36137=EDGE_LOOP ( 'NONE', ( #38640, #8921, #112849, #64653 ) ) ;
#36138=CARTESIAN_POINT ( 'NONE',  ( -9.183988606268997046, 28.73617430169793607, 5.000000000000000000 ) ) ;
#36139=CARTESIAN_POINT ( 'NONE',  ( 34.42499999999998295, 0.000000000000000000, 4.500000000000000888 ) ) ;
#36140=ORIENTED_EDGE ( 'NONE', *, *, #61936, .F. ) ;
#36141=PLANE ( 'NONE',  #140697 ) ;
#36142=EDGE_LOOP ( 'NONE', ( #78302, #41273, #22125, #94739 ) ) ;
#36143=ORIENTED_EDGE ( 'NONE', *, *, #72802, .F. ) ;
#36144=FACE_OUTER_BOUND ( 'NONE', #84147, .T. ) ;
#36148=ORIENTED_EDGE ( 'NONE', *, *, #136100, .F. ) ;
#36149=ADVANCED_FACE ( 'NONE', ( #65137 ), #96269, .T. ) ;
#36150=CARTESIAN_POINT ( 'NONE',  ( -5.187538124160488984, -22.22500000000000142, 4.000000000000000000 ) ) ;
#36152=DIRECTION ( 'NONE',  ( -0.6830127018922181881, 0.6830127018922202975, -0.2588190451025214056 ) ) ;
#36153=EDGE_CURVE ( 'NONE', #81705, #122500, #41204, .T. ) ;
#36154=DIRECTION ( 'NONE',  ( -0.7071067811865486830, -0.7071067811865464625, 0.000000000000000000 ) ) ;
#36156=CARTESIAN_POINT ( 'NONE',  ( -1.171830600776463838, 6.759292476615656575, 4.000000000000000000 ) ) ;
#36157=VECTOR ( 'NONE', #28036, 1000.000000000000000 ) ;
#36158=FACE_OUTER_BOUND ( 'NONE', #2121, .T. ) ;
#36160=EDGE_CURVE ( 'NONE', #49304, #2022, #30337, .T. ) ;
#36161=CARTESIAN_POINT ( 'NONE',  ( 34.49999999999976552, 4.464255608400454101, 4.994342998332159667 ) ) ;
#36162=VERTEX_POINT ( 'NONE', #120159 ) ;
#36163=CARTESIAN_POINT ( 'NONE',  ( 66.18398860626901126, 28.73617430169833753, 5.000000000000000000 ) ) ;
#36164=DIRECTION ( 'NONE',  ( 0.6830127018922180770, -0.6830127018922204085, -0.2588190451025213501 ) ) ;
#36165=ORIENTED_EDGE ( 'NONE', *, *, #56773, .T. ) ;
#36166=VERTEX_POINT ( 'NONE', #75293 ) ;
#36167=CARTESIAN_POINT ( 'NONE',  ( -22.49999999999983302, 16.46639925780209879, 5.000000000000000000 ) ) ;
#36168=ORIENTED_EDGE ( 'NONE', *, *, #75287, .F. ) ;
#36171=EDGE_CURVE ( 'NONE', #566, #4002, #44085, .T. ) ;
#36172=DIRECTION ( 'NONE',  ( 0.3543493200069162685, -0.000000000000000000, -0.9351131265310288487 ) ) ;
#36174=DIRECTION ( 'NONE',  ( 0.6830127018922180770, -0.6830127018922204085, -0.2588190451025213501 ) ) ;
#36175=ORIENTED_EDGE ( 'NONE', *, *, #121610, .F. ) ;
#36178=FACE_OUTER_BOUND ( 'NONE', #31978, .T. ) ;
#36181=VERTEX_POINT ( 'NONE', #128933 ) ;
#36182=EDGE_CURVE ( 'NONE', #118081, #127894, #41943, .T. ) ;
#36183=DIRECTION ( 'NONE',  ( 0.7071067811865487940, 0.7071067811865463515, -0.000000000000000000 ) ) ;
#36184=VECTOR ( 'NONE', #124534, 1000.000000000000000 ) ;
#36185=DIRECTION ( 'NONE',  ( -0.7071067811865486830, -0.7071067811865464625, 0.000000000000000000 ) ) ;
#36186=VERTEX_POINT ( 'NONE', #73844 ) ;
#36187=VERTEX_POINT ( 'NONE', #63000 ) ;
#36188=ORIENTED_EDGE ( 'NONE', *, *, #130696, .T. ) ;
#36189=CARTESIAN_POINT ( 'NONE',  ( -1.499999999999987566, -8.568876922607726598, 4.000000000000000000 ) ) ;
#36190=EDGE_CURVE ( 'NONE', #9326, #10796, #107174, .T. ) ;
#36191=FACE_OUTER_BOUND ( 'NONE', #120811, .T. ) ;
#36192=DIRECTION ( 'NONE',  ( -0.6830127018922180770, -0.6830127018922204085, -0.2588190451025213501 ) ) ;
#36194=CARTESIAN_POINT ( 'NONE',  ( 0.005480084712502889671, 28.92564299267938210, 4.000000000000000000 ) ) ;
#36195=LINE ( 'NONE', #56564, #36451 ) ;
#36196=DIRECTION ( 'NONE',  ( -0.7071067811865486830, -0.7071067811865464625, 0.000000000000000000 ) ) ;
#36197=DIRECTION ( 'NONE',  ( -0.000000000000000000, 0.3543493200069153248, 0.9351131265310292928 ) ) ;
#36198=VERTEX_POINT ( 'NONE', #12144 ) ;
#36199=EDGE_CURVE ( 'NONE', #86975, #70673, #22280, .T. ) ;
#36200=CARTESIAN_POINT ( 'NONE',  ( -34.49999999999975842, 22.08746187583901843, 4.000000000000000000 ) ) ;
#36201=ORIENTED_EDGE ( 'NONE', *, *, #74291, .F. ) ;
#36203=ORIENTED_EDGE ( 'NONE', *, *, #127176, .F. ) ;
#36205=ORIENTED_EDGE ( 'NONE', *, *, #31217, .T. ) ;
#36206=EDGE_CURVE ( 'NONE', #52654, #2296, #124485, .T. ) ;
#36207=LINE ( 'NONE', #69569, #132701 ) ;
#36209=ADVANCED_FACE ( 'NONE', ( #102024 ), #102747, .T. ) ;
#36210=ORIENTED_EDGE ( 'NONE', *, *, #48686, .F. ) ;
#36212=ORIENTED_EDGE ( 'NONE', *, *, #55197, .T. ) ;
#36213=AXIS2_PLACEMENT_3D ( 'NONE', #93132, #82976, #103274 ) ;
#36215=DIRECTION ( 'NONE',  ( -0.000000000000000000, 0.000000000000000000, 1.000000000000000000 ) ) ;
#36216=DIRECTION ( 'NONE',  ( -0.000000000000000000, 0.000000000000000000, 1.000000000000000000 ) ) ;
#36217=EDGE_CURVE ( 'NONE', #124676, #13638, #66547, .T. ) ;
#36218=CARTESIAN_POINT ( 'NONE',  ( -33.29974487139158867, -27.71228299555229313, 4.000000000000000000 ) ) ;
#36220=CARTESIAN_POINT ( 'NONE',  ( 54.18398860626899705, 28.73617430169825226, 5.000000000000000000 ) ) ;
#36221=FACE_OUTER_BOUND ( 'NONE', #19429, .T. ) ;
#36223=DIRECTION ( 'NONE',  ( -0.000000000000000000, 1.000000000000000000, -0.000000000000000000 ) ) ;
#36225=CARTESIAN_POINT ( 'NONE',  ( 54.18398860626899705, 28.73617430169825226, 5.000000000000000000 ) ) ;
#36226=DIRECTION ( 'NONE',  ( -0.3543493200069162685, -0.000000000000000000, -0.9351131265310288487 ) ) ;
#36227=VECTOR ( 'NONE', #135386, 1000.000000000000227 ) ;
#36228=EDGE_CURVE ( 'NONE', #73728, #140080, #68701, .T. ) ;
#36229=LINE ( 'NONE', #80455, #120739 ) ;
#36230=PLANE ( 'NONE',  #94044 ) ;
#36231=EDGE_LOOP ( 'NONE', ( #27364, #54235, #10106, #103006 ) ) ;
#36232=ORIENTED_EDGE ( 'NONE', *, *, #86404, .F. ) ;
#36234=ORIENTED_EDGE ( 'NONE', *, *, #36482, .F. ) ;
#36235=ORIENTED_EDGE ( 'NONE', *, *, #67824, .T. ) ;
#36236=VERTEX_POINT ( 'NONE', #77449 ) ;
#36237=CARTESIAN_POINT ( 'NONE',  ( -24.70710678118636139, -18.74070752338408852, 5.000000000000000000 ) ) ;
#36238=CARTESIAN_POINT ( 'NONE',  ( -34.92500000000001137, 5.816654386410375466, 4.500000000000000888 ) ) ;
#36239=LINE ( 'NONE', #68882, #31552 ) ;
#36240=ORIENTED_EDGE ( 'NONE', *, *, #92054, .F. ) ;
#36242=PLANE ( 'NONE',  #39560 ) ;
#36243=CARTESIAN_POINT ( 'NONE',  ( 0.000000000000000000, 0.000000000000000000, 5.000000000000000000 ) ) ;
#36244=DIRECTION ( 'NONE',  ( 0.7071067811865486830, -0.7071067811865464625, -0.000000000000000000 ) ) ;
#36245=FACE_OUTER_BOUND ( 'NONE', #17342, .T. ) ;
#36246=DIRECTION ( 'NONE',  ( 1.000000000000000000, 0.000000000000000000, 0.000000000000000000 ) ) ;
#36247=LINE ( 'NONE', #80477, #10283 ) ;
#36248=PLANE ( 'NONE',  #111611 ) ;
#36250=LINE ( 'NONE', #125399, #28396 ) ;
#36253=DIRECTION ( 'NONE',  ( 0.6830127018922181881, 0.6830127018922202975, -0.2588190451025214056 ) ) ;
#36254=ORIENTED_EDGE ( 'NONE', *, *, #91620, .F. ) ;
#36255=VERTEX_POINT ( 'NONE', #100608 ) ;
#36257=VECTOR ( 'NONE', #25266, 1000.000000000000227 ) ;
#36258=EDGE_LOOP ( 'NONE', ( #81019, #117487, #72812, #96289 ) ) ;
#36259=EDGE_CURVE ( 'NONE', #19670, #107544, #11397, .T. ) ;
#36260=DIRECTION ( 'NONE',  ( -0.3543493200069162685, -0.000000000000000000, -0.9351131265310288487 ) ) ;
#36262=LINE ( 'NONE', #123287, #15556 ) ;
#36263=AXIS2_PLACEMENT_3D ( 'NONE', #27943, #106182, #29353 ) ;
#36265=CARTESIAN_POINT ( 'NONE',  ( -26.99999999999980815, -19.44781430457063465, 5.000000000000000000 ) ) ;
#36268=VERTEX_POINT ( 'NONE', #45536 ) ;
#36269=CARTESIAN_POINT ( 'NONE',  ( 45.18398860626900415, 28.73617430169818832, 5.000000000000000000 ) ) ;
#36270=VECTOR ( 'NONE', #98946, 1000.000000000000000 ) ;
#36271=DIRECTION ( 'NONE',  ( -0.3543493200069163240, 4.681814790819596721E-17, -0.9351131265310288487 ) ) ;
#36273=ORIENTED_EDGE ( 'NONE', *, *, #141008, .T. ) ;
#36274=EDGE_CURVE ( 'NONE', #134985, #135515, #111461, .T. ) ;
#36275=EDGE_LOOP ( 'NONE', ( #116662, #65456, #4099, #136208 ) ) ;
#36277=EDGE_CURVE ( 'NONE', #33545, #108193, #23750, .T. ) ;
#36280=EDGE_LOOP ( 'NONE', ( #11678, #121479, #38536, #22817 ) ) ;
#36282=EDGE_CURVE ( 'NONE', #26660, #76331, #88305, .T. ) ;
#36283=ORIENTED_EDGE ( 'NONE', *, *, #123186, .F. ) ;
#36284=FACE_OUTER_BOUND ( 'NONE', #71984, .T. ) ;
#36285=ORIENTED_EDGE ( 'NONE', *, *, #47505, .T. ) ;
#36287=VERTEX_POINT ( 'NONE', #121612 ) ;
#36288=LINE ( 'NONE', #69651, #3073 ) ;
#36289=EDGE_CURVE ( 'NONE', #57345, #106069, #99878, .T. ) ;
#36290=CARTESIAN_POINT ( 'NONE',  ( -8.510786437626906675, -27.52281430457049183, 5.000000000000000000 ) ) ;
#36291=CARTESIAN_POINT ( 'NONE',  ( 6.938893903907228378E-15, 1.552185695429151080, 5.000000000000000000 ) ) ;
#36293=FACE_OUTER_BOUND ( 'NONE', #124424, .T. ) ;
#36294=DIRECTION ( 'NONE',  ( -0.000000000000000000, 0.3543493200069153248, 0.9351131265310292928 ) ) ;
#36295=EDGE_CURVE ( 'NONE', #94183, #6499, #544, .T. ) ;
#36297=VECTOR ( 'NONE', #18397, 1000.000000000000000 ) ;
#36298=FACE_BOUND ( 'NONE', #111974, .T. ) ;
#36299=ORIENTED_EDGE ( 'NONE', *, *, #71559, .F. ) ;
#36300=LINE ( 'NONE', #115229, #87495 ) ;
#36302=LINE ( 'NONE', #102984, #90829 ) ;
#36303=ORIENTED_EDGE ( 'NONE', *, *, #97767, .T. ) ;
#36304=CARTESIAN_POINT ( 'NONE',  ( 31.82816939922330945, 3.759292476615683665, 4.000000000000000000 ) ) ;
#36306=EDGE_CURVE ( 'NONE', #93602, #77576, #89029, .T. ) ;
#36307=ORIENTED_EDGE ( 'NONE', *, *, #56724, .F. ) ;
#36309=VERTEX_POINT ( 'NONE', #80297 ) ;
#36310=VECTOR ( 'NONE', #39322, 1000.000000000000000 ) ;
#36311=VECTOR ( 'NONE', #55329, 1000.000000000000000 ) ;
#36313=VERTEX_POINT ( 'NONE', #133247 ) ;
#36314=LINE ( 'NONE', #136321, #11634 ) ;
#36315=PLANE ( 'NONE',  #126094 ) ;
#36316=ADVANCED_FACE ( 'NONE', ( #13555 ), #33925, .T. ) ;
#36317=VERTEX_POINT ( 'NONE', #57125 ) ;
#36318=CARTESIAN_POINT ( 'NONE',  ( 33.48921356237309510, -27.52281430457078670, 5.000000000000000000 ) ) ;
#36319=FACE_OUTER_BOUND ( 'NONE', #8582, .T. ) ;
#36320=VECTOR ( 'NONE', #101671, 1000.000000000000000 ) ;
#36321=CARTESIAN_POINT ( 'NONE',  ( 11.99999999999991296, 10.21212019023810136, -2.019456568337826496 ) ) ;
#36323=ADVANCED_FACE ( 'NONE', ( #103423 ), #8202, .F. ) ;
#36324=CARTESIAN_POINT ( 'NONE',  ( 15.18398860626900237, 28.73617430169797871, 5.000000000000000000 ) ) ;
#36325=LINE ( 'NONE', #71109, #122725 ) ;
#36326=LINE ( 'NONE', #55955, #104956 ) ;
#36327=ORIENTED_EDGE ( 'NONE', *, *, #120380, .T. ) ;
#36331=CARTESIAN_POINT ( 'NONE',  ( 0.000000000000000000, 0.000000000000000000, 5.000000000000000000 ) ) ;
#36332=EDGE_LOOP ( 'NONE', ( #25328, #33665, #125621, #27262 ) ) ;
#36333=EDGE_CURVE ( 'NONE', #69752, #68093, #91847, .T. ) ;
#36334=ORIENTED_EDGE ( 'NONE', *, *, #50733, .T. ) ;
#36335=CARTESIAN_POINT ( 'NONE',  ( -5.908046338136182740, 22.22500000000000142, 15.99560845316876012 ) ) ;
#36336=ADVANCED_FACE ( 'NONE', ( #136072 ), #19112, .F. ) ;
#36337=EDGE_CURVE ( 'NONE', #29986, #100160, #64056, .T. ) ;
#36338=CARTESIAN_POINT ( 'NONE',  ( 29.99999999999979039, 13.93112307739203715, 4.000000000000000000 ) ) ;
#36339=VERTEX_POINT ( 'NONE', #4069 ) ;
#36343=LINE ( 'NONE', #89983, #127759 ) ;
#36345=AXIS2_PLACEMENT_3D ( 'NONE', #122816, #103196, #48126 ) ;
#36350=DIRECTION ( 'NONE',  ( -0.7071067811865486830, -0.7071067811865464625, 0.000000000000000000 ) ) ;
#36351=CARTESIAN_POINT ( 'NONE',  ( 12.79333936457838483, 21.75929247661549937, 4.998822639870715179 ) ) ;
#36352=ORIENTED_EDGE ( 'NONE', *, *, #139821, .F. ) ;
#36353=ORIENTED_EDGE ( 'NONE', *, *, #53457, .T. ) ;
#36354=VECTOR ( 'NONE', #5564, 1000.000000000000000 ) ;
#36355=DIRECTION ( 'NONE',  ( 0.7071067811865486830, -0.7071067811865464625, -0.000000000000000000 ) ) ;
#36356=DIRECTION ( 'NONE',  ( 0.6830127018922180770, -0.6830127018922204085, -0.2588190451025213501 ) ) ;
#36359=ADVANCED_FACE ( 'NONE', ( #92543 ), #127899, .F. ) ;
#36360=LINE ( 'NONE', #113905, #16912 ) ;
#36361=DIRECTION ( 'NONE',  ( -0.7071067811865486830, -0.7071067811865464625, -0.000000000000000000 ) ) ;
#36362=ORIENTED_EDGE ( 'NONE', *, *, #105600, .T. ) ;
#36363=FACE_OUTER_BOUND ( 'NONE', #27411, .T. ) ;
#36364=DIRECTION ( 'NONE',  ( 0.6830127018922181881, 0.6830127018922202975, -0.2588190451025214056 ) ) ;
#36365=DIRECTION ( 'NONE',  ( -0.000000000000000000, 0.000000000000000000, 1.000000000000000000 ) ) ;
#36366=VECTOR ( 'NONE', #29087, 1000.000000000000000 ) ;
#36367=ORIENTED_EDGE ( 'NONE', *, *, #134822, .T. ) ;
#36368=FACE_OUTER_BOUND ( 'NONE', #105559, .T. ) ;
#36369=LINE ( 'NONE', #24061, #67870 ) ;
#36370=ORIENTED_EDGE ( 'NONE', *, *, #143059, .F. ) ;
#36371=VECTOR ( 'NONE', #139904, 1000.000000000000000 ) ;
#36373=VERTEX_POINT ( 'NONE', #106817 ) ;
#36374=ORIENTED_EDGE ( 'NONE', *, *, #134348, .T. ) ;
#36376=CARTESIAN_POINT ( 'NONE',  ( -3.792893218813429446, -14.24070752338413826, 5.000000000000000000 ) ) ;
#36377=ORIENTED_EDGE ( 'NONE', *, *, #37649, .F. ) ;
#36378=EDGE_CURVE ( 'NONE', #86911, #68309, #40877, .T. ) ;
#36379=PLANE ( 'NONE',  #6745 ) ;
#36380=VECTOR ( 'NONE', #123329, 1000.000000000000000 ) ;
#36381=VERTEX_POINT ( 'NONE', #29977 ) ;
#36382=LINE ( 'NONE', #114631, #78551 ) ;
#36383=DIRECTION ( 'NONE',  ( 0.7071067811865486830, -0.7071067811865464625, -0.000000000000000000 ) ) ;
#36384=PLANE ( 'NONE',  #39771 ) ;
#36385=DIRECTION ( 'NONE',  ( 1.000000000000000000, 0.000000000000000000, 0.000000000000000000 ) ) ;
#36387=CARTESIAN_POINT ( 'NONE',  ( 8.999999999999941380, -3.033600742197707145, 5.000000000000000000 ) ) ;
#36388=LINE ( 'NONE', #124817, #47741 ) ;
#36389=EDGE_LOOP ( 'NONE', ( #121122, #1293, #139625, #86633 ) ) ;
#36391=ORIENTED_EDGE ( 'NONE', *, *, #4635, .F. ) ;
#36393=EDGE_LOOP ( 'NONE', ( #78071, #22616, #2586, #94508 ) ) ;
#36394=EDGE_LOOP ( 'NONE', ( #19985, #85200, #120642, #51973 ) ) ;
#36395=EDGE_LOOP ( 'NONE', ( #69009, #139042, #21391, #53054 ) ) ;
#36397=DIRECTION ( 'NONE',  ( -0.6830127018922180770, -0.6830127018922204085, -0.2588190451025213501 ) ) ;
#36399=PLANE ( 'NONE',  #55478 ) ;
#36402=VECTOR ( 'NONE', #57513, 1000.000000000000000 ) ;
#36403=FACE_OUTER_BOUND ( 'NONE', #58199, .T. ) ;
#36405=EDGE_LOOP ( 'NONE', ( #16341, #33344, #65031, #123384 ) ) ;
#36406=CARTESIAN_POINT ( 'NONE',  ( 23.57322811595262380, -0.7198850472490201380, 4.205258209906643785 ) ) ;
#36407=DIRECTION ( 'NONE',  ( -0.6830127018922180770, -0.6830127018922204085, -0.2588190451025213501 ) ) ;
#36408=CARTESIAN_POINT ( 'NONE',  ( 21.29974487139158512, -27.71228299555221142, 4.000000000000000000 ) ) ;
#36411=VECTOR ( 'NONE', #21767, 1000.000000000000000 ) ;
#36412=DIRECTION ( 'NONE',  ( 1.000000000000000000, 0.000000000000000000, 0.000000000000000000 ) ) ;
#36413=FACE_OUTER_BOUND ( 'NONE', #30955, .T. ) ;
#36414=VECTOR ( 'NONE', #8944, 1000.000000000000000 ) ;
#36416=DIRECTION ( 'NONE',  ( -0.3543493200069162685, -0.000000000000000000, -0.9351131265310288487 ) ) ;
#36419=EDGE_LOOP ( 'NONE', ( #137868, #17611, #132416, #2900 ) ) ;
#36420=ORIENTED_EDGE ( 'NONE', *, *, #31211, .T. ) ;
#36422=EDGE_LOOP ( 'NONE', ( #115202, #20323, #15249, #51765 ) ) ;
#36423=ORIENTED_EDGE ( 'NONE', *, *, #12699, .F. ) ;
#36424=DIRECTION ( 'NONE',  ( -0.000000000000000000, 0.000000000000000000, 1.000000000000000000 ) ) ;
#36425=DIRECTION ( 'NONE',  ( -0.7071067811865486830, 0.7071067811865464625, 0.000000000000000000 ) ) ;
#36426=VECTOR ( 'NONE', #141081, 1000.000000000000000 ) ;
#36427=ORIENTED_EDGE ( 'NONE', *, *, #33959, .T. ) ;
#36428=DIRECTION ( 'NONE',  ( -0.000000000000000000, 0.000000000000000000, 1.000000000000000000 ) ) ;
#36429=PLANE ( 'NONE',  #545 ) ;
#36431=ORIENTED_EDGE ( 'NONE', *, *, #110579, .T. ) ;
#36432=DIRECTION ( 'NONE',  ( -0.3543493200069163240, -0.000000000000000000, -0.9351131265310288487 ) ) ;
#36433=ORIENTED_EDGE ( 'NONE', *, *, #33995, .F. ) ;
#36435=CARTESIAN_POINT ( 'NONE',  ( -62.99451991528749772, 28.92564299267982264, 4.000000000000000000 ) ) ;
#36437=EDGE_CURVE ( 'NONE', #20187, #75689, #25888, .T. ) ;
#36438=LINE ( 'NONE', #88692, #118239 ) ;
#36439=ORIENTED_EDGE ( 'NONE', *, *, #37815, .T. ) ;
#36440=EDGE_CURVE ( 'NONE', #9403, #104700, #118409, .T. ) ;
#36441=ADVANCED_FACE ( 'NONE', ( #140870 ), #136786, .F. ) ;
#36442=EDGE_LOOP ( 'NONE', ( #127407, #69839, #128142, #40777 ) ) ;
#36443=FACE_OUTER_BOUND ( 'NONE', #52557, .T. ) ;
#36444=DIRECTION ( 'NONE',  ( -0.000000000000000000, 0.3543493200069152138, -0.9351131265310292928 ) ) ;
#36445=DIRECTION ( 'NONE',  ( -0.000000000000000000, 0.3543493200069153248, 0.9351131265310292928 ) ) ;
#36447=LINE ( 'NONE', #60365, #134285 ) ;
#36448=CARTESIAN_POINT ( 'NONE',  ( -68.99451991528748351, 28.92564299267986172, 4.000000000000000000 ) ) ;
#36450=EDGE_CURVE ( 'NONE', #101750, #49090, #143036, .T. ) ;
#36451=VECTOR ( 'NONE', #123215, 1000.000000000000000 ) ;
#36453=LINE ( 'NONE', #4456, #127427 ) ;
#36454=EDGE_CURVE ( 'NONE', #44302, #82135, #56063, .T. ) ;
#36455=DIRECTION ( 'NONE',  ( 1.000000000000000000, 0.000000000000000000, 0.000000000000000000 ) ) ;
#36456=EDGE_LOOP ( 'NONE', ( #47561, #143044, #60991, #20422 ) ) ;
#36457=ORIENTED_EDGE ( 'NONE', *, *, #17977, .F. ) ;
#36458=VECTOR ( 'NONE', #55529, 1000.000000000000000 ) ;
#36459=CARTESIAN_POINT ( 'NONE',  ( 31.49999999999977263, 8.319652575858409449, -8.582050562765751067 ) ) ;
#36460=EDGE_LOOP ( 'NONE', ( #75346, #66623, #54762, #72317 ) ) ;
#36462=ADVANCED_FACE ( 'NONE', ( #31429 ), #98800, .F. ) ;
#36463=LINE ( 'NONE', #68413, #127566 ) ;
#36464=ORIENTED_EDGE ( 'NONE', *, *, #27801, .F. ) ;
#36465=VECTOR ( 'NONE', #44267, 1000.000000000000114 ) ;
#36466=EDGE_CURVE ( 'NONE', #97559, #16532, #100253, .T. ) ;
#36468=FACE_BOUND ( 'NONE', #100319, .T. ) ;
#36470=DIRECTION ( 'NONE',  ( -0.7071067811865487940, 0.7071067811865463515, -0.000000000000000000 ) ) ;
#36471=LINE ( 'NONE', #119698, #85135 ) ;
#36472=LINE ( 'NONE', #3789, #138438 ) ;
#36473=ORIENTED_EDGE ( 'NONE', *, *, #126495, .T. ) ;
#36474=EDGE_CURVE ( 'NONE', #27138, #9302, #95091, .T. ) ;
#36475=CARTESIAN_POINT ( 'NONE',  ( 33.70710678118631165, -6.740707523384205757, 5.000000000000000000 ) ) ;
#36476=ORIENTED_EDGE ( 'NONE', *, *, #8183, .F. ) ;
#36479=ORIENTED_EDGE ( 'NONE', *, *, #62245, .F. ) ;
#36480=VECTOR ( 'NONE', #135613, 999.9999999999998863 ) ;
#36481=DIRECTION ( 'NONE',  ( 0.7071067811865487940, 0.7071067811865463515, -0.000000000000000000 ) ) ;
#36482=EDGE_CURVE ( 'NONE', #109252, #13343, #34280, .T. ) ;
#36483=EDGE_LOOP ( 'NONE', ( #74757, #80495, #52796, #61491 ) ) ;
#36485=DIRECTION ( 'NONE',  ( -0.7071067811865487940, 0.7071067811865463515, 0.000000000000000000 ) ) ;
#36486=EDGE_CURVE ( 'NONE', #138848, #106932, #33592, .T. ) ;
#36487=CARTESIAN_POINT ( 'NONE',  ( 34.42499999999998295, 1.541399257802028577, 5.000000000000000000 ) ) ;
#36489=CARTESIAN_POINT ( 'NONE',  ( -12.29974487139158512, -27.71228299555214747, 4.000000000000000000 ) ) ;
#36490=ADVANCED_FACE ( 'NONE', ( #23384 ), #53153, .F. ) ;
#36491=CARTESIAN_POINT ( 'NONE',  ( 9.328169399223456892, -18.74070752338409562, 4.000000000000000000 ) ) ;
#36492=CARTESIAN_POINT ( 'NONE',  ( -21.18398860626899349, 28.73617430169802134, 5.000000000000000000 ) ) ;
#36493=ORIENTED_EDGE ( 'NONE', *, *, #101440, .F. ) ;
#36494=EDGE_LOOP ( 'NONE', ( #131780, #68722, #3470, #106206 ) ) ;
#36496=VECTOR ( 'NONE', #15086, 1000.000000000000227 ) ;
#36497=CARTESIAN_POINT ( 'NONE',  ( 50.99451991528749062, 28.92564299267973738, 4.000000000000000000 ) ) ;
#36499=ADVANCED_FACE ( 'NONE', ( #8885 ), #54616, .F. ) ;
#36501=VECTOR ( 'NONE', #122199, 1000.000000000000227 ) ;
#36504=VERTEX_POINT ( 'NONE', #77793 ) ;
#36506=VECTOR ( 'NONE', #139202, 1000.000000000000000 ) ;
#36507=CARTESIAN_POINT ( 'NONE',  ( 26.99999999999981526, 7.552185695429090906, 5.000000000000000000 ) ) ;
#36509=DIRECTION ( 'NONE',  ( 0.3543493200069162685, -0.000000000000000000, -0.9351131265310288487 ) ) ;
#36510=ORIENTED_EDGE ( 'NONE', *, *, #38630, .T. ) ;
#36511=EDGE_CURVE ( 'NONE', #53146, #7053, #120531, .T. ) ;
#36512=CARTESIAN_POINT ( 'NONE',  ( -26.93988928955963402, -9.740707523384187994, 10.89222023123386940 ) ) ;
#36515=FACE_OUTER_BOUND ( 'NONE', #99944, .T. ) ;
#36516=DIRECTION ( 'NONE',  ( -0.7071067811865486830, 0.7071067811865464625, 0.000000000000000000 ) ) ;
#36519=LINE ( 'NONE', #27777, #128325 ) ;
#36520=DIRECTION ( 'NONE',  ( 0.7071067811865487940, 0.7071067811865463515, -0.000000000000000000 ) ) ;
#36521=CARTESIAN_POINT ( 'NONE',  ( 9.299744871391588674, -27.71228299555212971, 4.000000000000000000 ) ) ;
#36522=EDGE_LOOP ( 'NONE', ( #83862, #2774, #93455, #109891 ) ) ;
#36523=CARTESIAN_POINT ( 'NONE',  ( 18.18398860626898994, 28.73617430169800002, 5.000000000000000000 ) ) ;
#36524=DIRECTION ( 'NONE',  ( 0.7071067811865487940, 0.7071067811865463515, 0.000000000000000000 ) ) ;
#36525=CARTESIAN_POINT ( 'NONE',  ( -21.79289321881329755, -5.240707523384227073, 5.000000000000000000 ) ) ;
#36526=DIRECTION ( 'NONE',  ( 0.6830127018922181881, 0.6830127018922202975, -0.2588190451025214056 ) ) ;
#36527=LINE ( 'NONE', #12621, #142109 ) ;
#36528=ORIENTED_EDGE ( 'NONE', *, *, #53858, .T. ) ;
#36530=CARTESIAN_POINT ( 'NONE',  ( -25.56661756231483906, -22.22500000000000142, 8.546240940345063208 ) ) ;
#36531=DIRECTION ( 'NONE',  ( -0.7071067811865487940, 0.7071067811865463515, 0.000000000000000000 ) ) ;
#36532=PLANE ( 'NONE',  #3081 ) ;
#36535=ORIENTED_EDGE ( 'NONE', *, *, #136940, .T. ) ;
#36536=VERTEX_POINT ( 'NONE', #32876 ) ;
#36538=CARTESIAN_POINT ( 'NONE',  ( 30.72281430457039875, -21.72499999999999432, 5.000000000000000000 ) ) ;
#36539=DIRECTION ( 'NONE',  ( -0.000000000000000000, 0.000000000000000000, 1.000000000000000000 ) ) ;
#36541=LINE ( 'NONE', #27803, #6456 ) ;
#36543=CARTESIAN_POINT ( 'NONE',  ( 11.51078643762690490, -27.52281430457047406, 5.000000000000000000 ) ) ;
#36544=LINE ( 'NONE', #81508, #55241 ) ;
#36545=CARTESIAN_POINT ( 'NONE',  ( -32.29387692260781506, 22.22500000000000142, 4.000000000000000000 ) ) ;
#36546=ORIENTED_EDGE ( 'NONE', *, *, #56795, .T. ) ;
#36547=CARTESIAN_POINT ( 'NONE',  ( -20.51078643762690490, -27.52281430457041012, 5.000000000000000000 ) ) ;
#36548=LINE ( 'NONE', #27092, #37752 ) ;
#36549=DIRECTION ( 'NONE',  ( 0.7071067811865487940, -0.7071067811865463515, 0.000000000000000000 ) ) ;
#36551=LINE ( 'NONE', #70650, #106540 ) ;
#36552=EDGE_CURVE ( 'NONE', #31122, #99410, #141618, .T. ) ;
#36553=VERTEX_POINT ( 'NONE', #22644 ) ;
#36554=CARTESIAN_POINT ( 'NONE',  ( -5.994519915287488843, 28.92564299267942118, 4.000000000000000000 ) ) ;
#36555=ORIENTED_EDGE ( 'NONE', *, *, #79475, .T. ) ;
#36556=CARTESIAN_POINT ( 'NONE',  ( -8.999999999999932498, 5.966399257802200040, 5.000000000000000000 ) ) ;
#36557=DIRECTION ( 'NONE',  ( -0.000000000000000000, 0.3543493200069153248, 0.9351131265310292928 ) ) ;
#36558=DIRECTION ( 'NONE',  ( 0.6830127018922180770, -0.6830127018922204085, -0.2588190451025213501 ) ) ;
#36559=LINE ( 'NONE', #59767, #124918 ) ;
#36560=ADVANCED_FACE ( 'NONE', ( #89370 ), #42321, .F. ) ;
#36561=FACE_OUTER_BOUND ( 'NONE', #99751, .T. ) ;
#36563=ORIENTED_EDGE ( 'NONE', *, *, #59143, .T. ) ;
#36564=ORIENTED_EDGE ( 'NONE', *, *, #59432, .F. ) ;
#36566=DIRECTION ( 'NONE',  ( -0.7071067811865487940, 0.7071067811865463515, -0.000000000000000000 ) ) ;
#36567=CARTESIAN_POINT ( 'NONE',  ( 5.277185695429377432, -21.72500000000000853, 5.000000000000000000 ) ) ;
#36570=DIRECTION ( 'NONE',  ( -0.7071067811865486830, -0.7071067811865464625, 0.000000000000000000 ) ) ;
#36571=ORIENTED_EDGE ( 'NONE', *, *, #82180, .F. ) ;
#36572=VECTOR ( 'NONE', #130457, 999.9999999999998863 ) ;
#36574=DIRECTION ( 'NONE',  ( -1.000000000000000000, 0.000000000000000000, -0.000000000000000000 ) ) ;
#36575=CARTESIAN_POINT ( 'NONE',  ( 19.49999999999987210, 13.08746187583910725, 4.000000000000000000 ) ) ;
#36576=LINE ( 'NONE', #59785, #100685 ) ;
#36577=EDGE_LOOP ( 'NONE', ( #135875, #16772, #47586, #12639 ) ) ;
#36578=CARTESIAN_POINT ( 'NONE',  ( 24.79333936457830134, 21.75929247661549226, 4.998822639870711626 ) ) ;
#36582=CARTESIAN_POINT ( 'NONE',  ( -48.18398860626899705, 28.73617430169820608, 5.000000000000000000 ) ) ;
#36583=VERTEX_POINT ( 'NONE', #64771 ) ;
#36584=ORIENTED_EDGE ( 'NONE', *, *, #27142, .T. ) ;
#36585=CARTESIAN_POINT ( 'NONE',  ( 78.48921356237309510, -27.52281430457109934, 5.000000000000000000 ) ) ;
#36586=CARTESIAN_POINT ( 'NONE',  ( 18.41161490594819128, 22.22500000000000142, 4.777194822843815913 ) ) ;
#36588=LINE ( 'NONE', #56959, #94950 ) ;
#36590=EDGE_CURVE ( 'NONE', #95889, #56990, #32132, .T. ) ;
#36591=DIRECTION ( 'NONE',  ( 0.6830127018922180770, -0.6830127018922204085, -0.2588190451025214056 ) ) ;
#36592=ORIENTED_EDGE ( 'NONE', *, *, #41185, .T. ) ;
#36596=AXIS2_PLACEMENT_3D ( 'NONE', #119721, #121870, #32770 ) ;
#36597=AXIS2_PLACEMENT_3D ( 'NONE', #26140, #124026, #82667 ) ;
#36599=ORIENTED_EDGE ( 'NONE', *, *, #112417, .T. ) ;
#36600=EDGE_CURVE ( 'NONE', #68320, #25758, #21961, .T. ) ;
#36603=( BOUNDED_CURVE ( )  B_SPLINE_CURVE ( 3, ( #139360, #83539, #84263, #71961 ),
 .UNSPECIFIED., .F., .T. ) 
 B_SPLINE_CURVE_WITH_KNOTS ( ( 4, 4 ),
 ( 5.005968288816718292, 5.074607125596354962 ),
 .UNSPECIFIED. ) 
 CURVE ( )  GEOMETRIC_REPRESENTATION_ITEM ( )  RATIONAL_B_SPLINE_CURVE ( ( 1.000000000000000000, 0.9996074310407762065, 0.9996074310407762065, 1.000000000000000000 ) ) 
 REPRESENTATION_ITEM ( '' )  );
#36605=DIRECTION ( 'NONE',  ( -0.7071067811865486830, -0.7071067811865464625, 0.000000000000000000 ) ) ;
#36606=EDGE_CURVE ( 'NONE', #85671, #142121, #135056, .T. ) ;
#36608=LINE ( 'NONE', #111308, #103430 ) ;
#36609=ORIENTED_EDGE ( 'NONE', *, *, #49325, .T. ) ;
#36610=ORIENTED_EDGE ( 'NONE', *, *, #96612, .F. ) ;
#36611=EDGE_CURVE ( 'NONE', #22039, #21922, #126285, .T. ) ;
#36612=CARTESIAN_POINT ( 'NONE',  ( 5.816011393731002066, 28.73617430169783304, 5.000000000000000000 ) ) ;
#36614=EDGE_CURVE ( 'NONE', #111099, #13267, #44599, .T. ) ;
#36615=ORIENTED_EDGE ( 'NONE', *, *, #1564, .T. ) ;
#36618=CARTESIAN_POINT ( 'NONE',  ( -2.816011393730999401, 28.73617430169785436, 5.000000000000000000 ) ) ;
#36619=DIRECTION ( 'NONE',  ( -0.000000000000000000, 0.000000000000000000, 1.000000000000000000 ) ) ;
#36621=VECTOR ( 'NONE', #71325, 1000.000000000000114 ) ;
#36622=ADVANCED_FACE ( 'NONE', ( #21375 ), #77210, .F. ) ;
#36623=FACE_BOUND ( 'NONE', #36258, .T. ) ;
#36625=LINE ( 'NONE', #44713, #60626 ) ;
#36626=DIRECTION ( 'NONE',  ( -0.7071067811865486830, -0.7071067811865464625, -0.000000000000000000 ) ) ;
#36627=VECTOR ( 'NONE', #18823, 1000.000000000000000 ) ;
#36628=CARTESIAN_POINT ( 'NONE',  ( -12.29974487139158512, -27.71228299555214747, 4.000000000000000000 ) ) ;
#36629=EDGE_CURVE ( 'NONE', #95062, #28555, #19924, .T. ) ;
#36630=CARTESIAN_POINT ( 'NONE',  ( 17.20710678118642534, -14.24070752338414181, 5.000000000000000000 ) ) ;
#36632=ORIENTED_EDGE ( 'NONE', *, *, #12093, .T. ) ;
#36633=EDGE_LOOP ( 'NONE', ( #132694, #17206, #36285, #90556 ) ) ;
#36636=CARTESIAN_POINT ( 'NONE',  ( 30.48921356237309510, -27.52281430457076894, 5.000000000000000000 ) ) ;
#36637=LINE ( 'NONE', #104756, #35212 ) ;
#36638=VECTOR ( 'NONE', #97059, 1000.000000000000000 ) ;
#36639=CARTESIAN_POINT ( 'NONE',  ( 17.20666063542140733, 21.75929247661550292, 4.998822639870701856 ) ) ;
#36640=AXIS2_PLACEMENT_3D ( 'NONE', #36033, #46940, #124437 ) ;
#36641=CARTESIAN_POINT ( 'NONE',  ( 34.42499999999998295, -21.72500000000000142, 4.500000000000000888 ) ) ;
#36642=EDGE_LOOP ( 'NONE', ( #44160, #67527, #64982, #59692, #134697, #89303, #87881, #59506 ) ) ;
#36644=CARTESIAN_POINT ( 'NONE',  ( -34.92500000000001137, 22.22500000000000142, 4.000000000000000000 ) ) ;
#36645=CARTESIAN_POINT ( 'NONE',  ( 19.22674160717822289, -11.24070752338415780, 18.24660765846986621 ) ) ;
#36648=ADVANCED_FACE ( 'NONE', ( #33698 ), #109804, .F. ) ;
#36649=CARTESIAN_POINT ( 'NONE',  ( 16.92580874392867685, 8.754106587137664874, 4.662926800793069759 ) ) ;
#36650=CARTESIAN_POINT ( 'NONE',  ( 34.17183060077622514, 12.75929247661558641, 4.000000000000000000 ) ) ;
#36651=ORIENTED_EDGE ( 'NONE', *, *, #61278, .F. ) ;
#36652=DIRECTION ( 'NONE',  ( -0.7071067811865486830, -0.7071067811865464625, 0.000000000000000000 ) ) ;
#36654=LINE ( 'NONE', #14900, #14104 ) ;
#36657=ORIENTED_EDGE ( 'NONE', *, *, #78775, .T. ) ;
#36660=EDGE_CURVE ( 'NONE', #128291, #13057, #22752, .T. ) ;
#36662=VECTOR ( 'NONE', #98870, 1000.000000000000227 ) ;
#36664=VERTEX_POINT ( 'NONE', #132308 ) ;
#36666=DIRECTION ( 'NONE',  ( -0.000000000000000000, 0.3543493200069153248, 0.9351131265310292928 ) ) ;
#36667=VERTEX_POINT ( 'NONE', #42440 ) ;
#36668=DIRECTION ( 'NONE',  ( 0.6830127018922180770, -0.6830127018922204085, -0.2588190451025213501 ) ) ;
#36669=LINE ( 'NONE', #45453, #88781 ) ;
#36670=EDGE_LOOP ( 'NONE', ( #16278, #723, #102002, #80716 ) ) ;
#36672=CARTESIAN_POINT ( 'NONE',  ( 23.99451991528749062, 28.92564299267954908, 4.000000000000000000 ) ) ;
#36673=CARTESIAN_POINT ( 'NONE',  ( 32.29289321881323360, 8.259292476615643253, 5.000000000000000000 ) ) ;
#36675=ORIENTED_EDGE ( 'NONE', *, *, #13152, .T. ) ;
#36676=DIRECTION ( 'NONE',  ( -0.6830127018922181881, 0.6830127018922202975, -0.2588190451025214056 ) ) ;
#36677=ORIENTED_EDGE ( 'NONE', *, *, #88721, .T. ) ;
#36678=ORIENTED_EDGE ( 'NONE', *, *, #105022, .T. ) ;
#36679=ORIENTED_EDGE ( 'NONE', *, *, #126743, .T. ) ;
#36680=CARTESIAN_POINT ( 'NONE',  ( -28.49999999999980460, -12.08601207473291161, -10.46905243149087461 ) ) ;
#36681=VECTOR ( 'NONE', #41261, 1000.000000000000000 ) ;
#36682=VECTOR ( 'NONE', #115111, 1000.000000000000000 ) ;
#36683=DIRECTION ( 'NONE',  ( -0.000000000000000000, -0.3543493200069152693, 0.9351131265310292928 ) ) ;
#36684=VECTOR ( 'NONE', #97220, 999.9999999999998863 ) ;
#36685=LINE ( 'NONE', #105502, #58717 ) ;
#36686=EDGE_CURVE ( 'NONE', #69641, #64405, #130872, .T. ) ;
#36687=CARTESIAN_POINT ( 'NONE',  ( 74.99451991528749772, 28.92564299267990435, 4.000000000000000000 ) ) ;
#36688=AXIS2_PLACEMENT_3D ( 'NONE', #143333, #77406, #88256 ) ;
#36689=EDGE_CURVE ( 'NONE', #91593, #44215, #142451, .T. ) ;
#36690=DIRECTION ( 'NONE',  ( -0.7071067811865487940, 0.7071067811865463515, 0.000000000000000000 ) ) ;
#36691=ORIENTED_EDGE ( 'NONE', *, *, #99676, .T. ) ;
#36692=VECTOR ( 'NONE', #77538, 1000.000000000000000 ) ;
#36693=VECTOR ( 'NONE', #57664, 1000.000000000000000 ) ;
#36694=DIRECTION ( 'NONE',  ( -0.7071067811865487940, 0.7071067811865463515, 0.000000000000000000 ) ) ;
#36696=PLANE ( 'NONE',  #23093 ) ;
#36697=DIRECTION ( 'NONE',  ( 1.000000000000000000, 0.000000000000000000, 0.000000000000000000 ) ) ;
#36698=CARTESIAN_POINT ( 'NONE',  ( -5.292986735706916690, -21.74070752338406010, 4.999753212805220670 ) ) ;
#36700=ORIENTED_EDGE ( 'NONE', *, *, #17324, .T. ) ;
#36701=ORIENTED_EDGE ( 'NONE', *, *, #142187, .T. ) ;
#36703=DIRECTION ( 'NONE',  ( -0.7071067811865486830, -0.7071067811865464625, -0.000000000000000000 ) ) ;
#36706=CARTESIAN_POINT ( 'NONE',  ( -69.18398860626899705, 28.73617430169835529, 5.000000000000000000 ) ) ;
#36707=DIRECTION ( 'NONE',  ( -0.7071067811865486830, -0.7071067811865464625, 0.000000000000000000 ) ) ;
#36710=DIRECTION ( 'NONE',  ( 1.000000000000000000, 0.000000000000000000, 0.000000000000000000 ) ) ;
#36712=CARTESIAN_POINT ( 'NONE',  ( -22.41009064519818494, 9.759292476615618384, 11.28811694763773588 ) ) ;
#36713=EDGE_CURVE ( 'NONE', #22536, #121049, #140987, .T. ) ;
#36714=DIRECTION ( 'NONE',  ( -0.7071067811865487940, 0.7071067811865463515, -0.000000000000000000 ) ) ;
#36715=CARTESIAN_POINT ( 'NONE',  ( 6.792893218813405909, 15.75929247661555976, 5.000000000000000000 ) ) ;
#36716=DIRECTION ( 'NONE',  ( -0.000000000000000000, 0.3543493200069153248, 0.9351131265310292928 ) ) ;
#36717=CARTESIAN_POINT ( 'NONE',  ( -19.49999999999986855, 19.39370406404965408, 1.459788787078246886 ) ) ;
#36718=EDGE_LOOP ( 'NONE', ( #117080, #82200, #130530, #61167 ) ) ;
#36719=VECTOR ( 'NONE', #125368, 1000.000000000000000 ) ;
#36721=EDGE_LOOP ( 'NONE', ( #10631, #1331, #76070, #43260 ) ) ;
#36722=VECTOR ( 'NONE', #70815, 1000.000000000000227 ) ;
#36723=VECTOR ( 'NONE', #65232, 1000.000000000000227 ) ;
#36724=DIRECTION ( 'NONE',  ( 0.7071067811865487940, -0.7071067811865463515, 0.000000000000000000 ) ) ;
#36725=DIRECTION ( 'NONE',  ( 0.7071067811865486830, -0.7071067811865464625, -0.000000000000000000 ) ) ;
#36726=EDGE_LOOP ( 'NONE', ( #104431, #137592, #86162, #46270 ) ) ;
#36727=EDGE_CURVE ( 'NONE', #54018, #6851, #20638, .T. ) ;
#36728=LINE ( 'NONE', #68676, #33367 ) ;
#36730=PLANE ( 'NONE',  #20659 ) ;
#36731=ORIENTED_EDGE ( 'NONE', *, *, #132604, .T. ) ;
#36733=EDGE_LOOP ( 'NONE', ( #91542, #48998, #37066, #39176 ) ) ;
#36735=VECTOR ( 'NONE', #112973, 999.9999999999998863 ) ;
#36736=CARTESIAN_POINT ( 'NONE',  ( 7.499999999999951150, -7.420205493532891161, -2.617629953481236615 ) ) ;
#36738=DIRECTION ( 'NONE',  ( -0.6830127018922180770, -0.6830127018922204085, -0.2588190451025213501 ) ) ;
#36740=ORIENTED_EDGE ( 'NONE', *, *, #54143, .T. ) ;
#36741=LINE ( 'NONE', #69396, #88608 ) ;
#36742=DIRECTION ( 'NONE',  ( 0.7071067811865486830, -0.7071067811865464625, -0.000000000000000000 ) ) ;
#36743=CARTESIAN_POINT ( 'NONE',  ( 33.45983838949720024, 18.75929247661552779, 8.305906642995562805 ) ) ;
#36745=DIRECTION ( 'NONE',  ( -0.000000000000000000, 0.000000000000000000, 1.000000000000000000 ) ) ;
#36746=VECTOR ( 'NONE', #23509, 999.9999999999998863 ) ;
#36748=DIRECTION ( 'NONE',  ( 0.000000000000000000, 1.000000000000000000, 0.000000000000000000 ) ) ;
#36750=CARTESIAN_POINT ( 'NONE',  ( 36.48921356237310221, -27.52281430457080802, 5.000000000000000000 ) ) ;
#36751=VERTEX_POINT ( 'NONE', #88790 ) ;
#36753=CARTESIAN_POINT ( 'NONE',  ( 3.516654386410431599, 22.22500000000000142, 4.500000000000000888 ) ) ;
#36754=DIRECTION ( 'NONE',  ( -0.7071067811865487940, 0.7071067811865463515, -0.000000000000000000 ) ) ;
#36755=DIRECTION ( 'NONE',  ( 0.7071067811865486830, -0.7071067811865464625, -0.000000000000000000 ) ) ;
#36756=CARTESIAN_POINT ( 'NONE',  ( 6.938893903907228378E-15, 14.96639925780210767, 5.000000000000000000 ) ) ;
#36757=ORIENTED_EDGE ( 'NONE', *, *, #54193, .F. ) ;
#36758=CARTESIAN_POINT ( 'NONE',  ( 3.792893218813436551, -11.24070752338417201, 5.000000000000000000 ) ) ;
#36759=ORIENTED_EDGE ( 'NONE', *, *, #135511, .T. ) ;
#36760=LINE ( 'NONE', #57136, #32382 ) ;
#36761=CARTESIAN_POINT ( 'NONE',  ( 14.20666063542142687, 21.75929247661549937, 4.998822639870700080 ) ) ;
#36762=DIRECTION ( 'NONE',  ( -0.7071067811865486830, -0.7071067811865464625, 0.000000000000000000 ) ) ;
#36763=ORIENTED_EDGE ( 'NONE', *, *, #135841, .F. ) ;
#36764=DIRECTION ( 'NONE',  ( 0.7071067811865486830, -0.7071067811865464625, -0.000000000000000000 ) ) ;
#36765=CARTESIAN_POINT ( 'NONE',  ( -7.499999999999940492, 4.087461875839200509, 4.000000000000000000 ) ) ;
#36766=DIRECTION ( 'NONE',  ( 0.6830127018922181881, 0.6830127018922202975, -0.2588190451025214056 ) ) ;
#36767=FACE_OUTER_BOUND ( 'NONE', #5161, .T. ) ;
#36770=ORIENTED_EDGE ( 'NONE', *, *, #41838, .F. ) ;
#36771=EDGE_CURVE ( 'NONE', #34970, #86645, #143404, .T. ) ;
#36773=ORIENTED_EDGE ( 'NONE', *, *, #51544, .F. ) ;
#36774=ADVANCED_FACE ( 'NONE', ( #32253 ), #130149, .F. ) ;
#36775=EDGE_CURVE ( 'NONE', #84947, #34514, #43138, .T. ) ;
#36776=CARTESIAN_POINT ( 'NONE',  ( 0.4892135623730947680, -27.52281430457055578, 5.000000000000000000 ) ) ;
#36777=DIRECTION ( 'NONE',  ( 0.7071067811865486830, -0.7071067811865464625, -0.000000000000000000 ) ) ;
#36780=DIRECTION ( 'NONE',  ( 0.7071067811865487940, 0.7071067811865463515, 0.000000000000000000 ) ) ;
#36781=VERTEX_POINT ( 'NONE', #143144 ) ;
#36782=ADVANCED_FACE ( 'NONE', ( #43844 ), #13320, .F. ) ;
#36783=CARTESIAN_POINT ( 'NONE',  ( -38.99451991528749062, 28.92564299267965211, 4.000000000000000000 ) ) ;
#36784=LINE ( 'NONE', #33958, #102216 ) ;
#36786=EDGE_LOOP ( 'NONE', ( #89808, #27678, #15416, #61529 ) ) ;
#36787=VECTOR ( 'NONE', #121040, 1000.000000000000000 ) ;
#36789=CARTESIAN_POINT ( 'NONE',  ( -21.48921356237309155, -27.52281430457070499, 5.000000000000000000 ) ) ;
#36790=LINE ( 'NONE', #55177, #22396 ) ;
#36791=DIRECTION ( 'NONE',  ( 0.3543493200069162685, -0.000000000000000000, -0.9351131265310288487 ) ) ;
#36792=VECTOR ( 'NONE', #64842, 1000.000000000000000 ) ;
#36793=VECTOR ( 'NONE', #8325, 1000.000000000000000 ) ;
#36794=AXIS2_PLACEMENT_3D ( 'NONE', #103646, #105101, #18050 ) ;
#36795=ORIENTED_EDGE ( 'NONE', *, *, #17314, .F. ) ;
#36796=ORIENTED_EDGE ( 'NONE', *, *, #95378, .T. ) ;
#36798=EDGE_CURVE ( 'NONE', #33598, #141915, #37245, .T. ) ;
#36799=DIRECTION ( 'NONE',  ( 0.6830127018922181881, 0.6830127018922202975, -0.2588190451025214056 ) ) ;
#36800=EDGE_CURVE ( 'NONE', #111053, #105971, #14773, .T. ) ;
#36802=CARTESIAN_POINT ( 'NONE',  ( 4.828169399223495084, -14.24070752338413648, 4.000000000000000000 ) ) ;
#36803=VECTOR ( 'NONE', #94310, 1000.000000000000000 ) ;
#36805=EDGE_CURVE ( 'NONE', #101569, #4002, #46003, .T. ) ;
#36806=FACE_OUTER_BOUND ( 'NONE', #45433, .T. ) ;
#36807=CARTESIAN_POINT ( 'NONE',  ( -11.99999999999992006, -7.068876922607741697, 4.000000000000000000 ) ) ;
#36809=ORIENTED_EDGE ( 'NONE', *, *, #34882, .T. ) ;
#36810=CARTESIAN_POINT ( 'NONE',  ( -1.499999999999990896, -14.56887692260766443, 4.000000000000000000 ) ) ;
#36811=EDGE_LOOP ( 'NONE', ( #59704, #116421, #114878, #60761 ) ) ;
#36814=FACE_OUTER_BOUND ( 'NONE', #77747, .T. ) ;
#36815=ORIENTED_EDGE ( 'NONE', *, *, #97259, .F. ) ;
#36816=DIRECTION ( 'NONE',  ( -0.7071067811865487940, 0.7071067811865463515, 0.000000000000000000 ) ) ;
#36817=FACE_OUTER_BOUND ( 'NONE', #69566, .T. ) ;
#36818=EDGE_CURVE ( 'NONE', #35075, #103659, #69918, .T. ) ;
#36819=PLANE ( 'NONE',  #90189 ) ;
#36820=AXIS2_PLACEMENT_3D ( 'NONE', #80845, #57676, #101858 ) ;
#36821=CARTESIAN_POINT ( 'NONE',  ( -16.49999999999988987, 22.22500000000000853, 4.362957392718826988 ) ) ;
#36823=VECTOR ( 'NONE', #124285, 1000.000000000000000 ) ;
#36824=DIRECTION ( 'NONE',  ( -0.7071067811865486830, -0.7071067811865464625, 0.000000000000000000 ) ) ;
#36826=VERTEX_POINT ( 'NONE', #14041 ) ;
#36827=DIRECTION ( 'NONE',  ( -0.6830127018922180770, -0.6830127018922204085, -0.2588190451025213501 ) ) ;
#36828=ORIENTED_EDGE ( 'NONE', *, *, #20755, .T. ) ;
#36829=ORIENTED_EDGE ( 'NONE', *, *, #26100, .F. ) ;
#36830=CARTESIAN_POINT ( 'NONE',  ( 29.99999999999979039, 18.08204922493375477, 0.9627537363044178509 ) ) ;
#36831=ORIENTED_EDGE ( 'NONE', *, *, #125123, .T. ) ;
#36832=VERTEX_POINT ( 'NONE', #122825 ) ;
#36834=ORIENTED_EDGE ( 'NONE', *, *, #7869, .T. ) ;
#36837=CARTESIAN_POINT ( 'NONE',  ( 20.99999999999985789, 16.93112307739201583, 4.000000000000000000 ) ) ;
#36838=CARTESIAN_POINT ( 'NONE',  ( -59.99451991528749772, 28.92564299267980132, 4.000000000000000000 ) ) ;
#36840=CARTESIAN_POINT ( 'NONE',  ( -48.18398860626899705, 28.73617430169820608, 5.000000000000000000 ) ) ;
#36841=EDGE_CURVE ( 'NONE', #41034, #13806, #53616, .T. ) ;
#36842=CARTESIAN_POINT ( 'NONE',  ( -51.29974487139158867, -27.71228299555242103, 4.000000000000000000 ) ) ;
#36843=DIRECTION ( 'NONE',  ( 0.3543493200069162685, -0.000000000000000000, -0.9351131265310288487 ) ) ;
#36845=PLANE ( 'NONE',  #56314 ) ;
#36847=LINE ( 'NONE', #15761, #39013 ) ;
#36848=ORIENTED_EDGE ( 'NONE', *, *, #86219, .T. ) ;
#36850=EDGE_CURVE ( 'NONE', #68092, #93258, #12622, .T. ) ;
#36851=EDGE_LOOP ( 'NONE', ( #116800, #48598, #93268, #105089 ) ) ;
#36852=ORIENTED_EDGE ( 'NONE', *, *, #77404, .F. ) ;
#36853=CARTESIAN_POINT ( 'NONE',  ( 7.828169399223476432, 12.75929247661558996, 4.000000000000000000 ) ) ;
#36854=ORIENTED_EDGE ( 'NONE', *, *, #49916, .F. ) ;
#36855=DIRECTION ( 'NONE',  ( 0.7071067811865486830, -0.7071067811865464625, -0.000000000000000000 ) ) ;
#36859=DIRECTION ( 'NONE',  ( 0.6830127018922180770, -0.6830127018922204085, -0.2588190451025213501 ) ) ;
#36860=ORIENTED_EDGE ( 'NONE', *, *, #91229, .F. ) ;
#36861=CARTESIAN_POINT ( 'NONE',  ( -27.29974487139158512, -27.71228299555225405, 4.000000000000000000 ) ) ;
#36862=ORIENTED_EDGE ( 'NONE', *, *, #34820, .T. ) ;
#36863=PLANE ( 'NONE',  #104758 ) ;
#36866=CARTESIAN_POINT ( 'NONE',  ( -33.70710678118631165, 14.25929247661557397, 5.000000000000000000 ) ) ;
#36867=ORIENTED_EDGE ( 'NONE', *, *, #121567, .F. ) ;
#36869=VERTEX_POINT ( 'NONE', #135162 ) ;
#36872=DIRECTION ( 'NONE',  ( -0.7071067811865487940, 0.7071067811865463515, -0.000000000000000000 ) ) ;
#36873=LINE ( 'NONE', #69549, #139901 ) ;
#36874=ORIENTED_EDGE ( 'NONE', *, *, #93914, .T. ) ;
#36875=DIRECTION ( 'NONE',  ( 0.7071067811865487940, 0.7071067811865463515, 0.000000000000000000 ) ) ;
#36876=LINE ( 'NONE', #49224, #1723 ) ;
#36877=EDGE_CURVE ( 'NONE', #37329, #22290, #45301, .T. ) ;
#36878=LINE ( 'NONE', #4927, #46683 ) ;
#36880=CARTESIAN_POINT ( 'NONE',  ( 34.92499999999998295, -9.183345613589446899, 4.500000000000000888 ) ) ;
#36881=ORIENTED_EDGE ( 'NONE', *, *, #68873, .F. ) ;
#36882=VECTOR ( 'NONE', #21101, 1000.000000000000000 ) ;
#36883=VECTOR ( 'NONE', #113328, 999.9999999999998863 ) ;
#36884=VECTOR ( 'NONE', #27804, 1000.000000000000000 ) ;
#36885=VECTOR ( 'NONE', #84423, 1000.000000000000227 ) ;
#36887=ORIENTED_EDGE ( 'NONE', *, *, #104810, .F. ) ;
#36888=( BOUNDED_CURVE ( )  B_SPLINE_CURVE ( 3, ( #46367, #136898, #2056, #57952 ),
 .UNSPECIFIED., .F., .F. ) 
 B_SPLINE_CURVE_WITH_KNOTS ( ( 4, 4 ),
 ( 5.536208752217765650, 5.573248253235213667 ),
 .UNSPECIFIED. ) 
 CURVE ( )  GEOMETRIC_REPRESENTATION_ITEM ( )  RATIONAL_B_SPLINE_CURVE ( ( 1.000000000000000000, 0.9998856762146628441, 0.9998856762146628441, 1.000000000000000000 ) ) 
 REPRESENTATION_ITEM ( '' )  );
#36889=VECTOR ( 'NONE', #114894, 1000.000000000000227 ) ;
#36890=EDGE_CURVE ( 'NONE', #109601, #101394, #46753, .T. ) ;
#36891=CARTESIAN_POINT ( 'NONE',  ( -20.99999999999985789, 15.45873954670183004, -0.03131636524289407170 ) ) ;
#36892=ORIENTED_EDGE ( 'NONE', *, *, #50718, .T. ) ;
#36893=VERTEX_POINT ( 'NONE', #69174 ) ;
#36894=EDGE_CURVE ( 'NONE', #74888, #85582, #1020, .T. ) ;
#36895=DIRECTION ( 'NONE',  ( 0.7071067811865487940, 0.7071067811865463515, -0.000000000000000000 ) ) ;
#36897=ORIENTED_EDGE ( 'NONE', *, *, #5956, .F. ) ;
#36899=AXIS2_PLACEMENT_3D ( 'NONE', #695, #133392, #23151 ) ;
#36900=EDGE_LOOP ( 'NONE', ( #62119, #120729, #21318, #26267 ) ) ;
#36901=CARTESIAN_POINT ( 'NONE',  ( 15.45983838949730860, 18.75929247661552779, 8.305906642995520173 ) ) ;
#36902=FACE_OUTER_BOUND ( 'NONE', #17251, .T. ) ;
#36904=CARTESIAN_POINT ( 'NONE',  ( -18.48921356237309510, -27.52281430457068367, 5.000000000000000000 ) ) ;
#36905=DIRECTION ( 'NONE',  ( -0.3543493200069162685, -0.000000000000000000, -0.9351131265310288487 ) ) ;
#36906=FACE_OUTER_BOUND ( 'NONE', #76600, .T. ) ;
#36907=CARTESIAN_POINT ( 'NONE',  ( -30.15612307739222331, -22.22500000000000853, 4.000000000000000000 ) ) ;
#36908=DIRECTION ( 'NONE',  ( 0.7071067811865487940, 0.7071067811865463515, 0.000000000000000000 ) ) ;
#36909=DIRECTION ( 'NONE',  ( -0.7071067811865486830, 0.7071067811865464625, 0.000000000000000000 ) ) ;
#36912=VECTOR ( 'NONE', #23720, 1000.000000000000000 ) ;
#36913=CARTESIAN_POINT ( 'NONE',  ( -15.32816939922343202, 11.25929247661560595, 4.000000000000000000 ) ) ;
#36914=VECTOR ( 'NONE', #90936, 1000.000000000000000 ) ;
#36915=CARTESIAN_POINT ( 'NONE',  ( 48.48921356237309510, -27.52281430457089328, 5.000000000000000000 ) ) ;
#36916=DIRECTION ( 'NONE',  ( 1.000000000000000000, 0.000000000000000000, 0.000000000000000000 ) ) ;
#36917=EDGE_LOOP ( 'NONE', ( #139450, #21444, #78577, #136144 ) ) ;
#36919=VERTEX_POINT ( 'NONE', #89476 ) ;
#36921=VECTOR ( 'NONE', #137334, 999.9999999999998863 ) ;
#36922=ORIENTED_EDGE ( 'NONE', *, *, #71221, .F. ) ;
#36923=ORIENTED_EDGE ( 'NONE', *, *, #43045, .F. ) ;
#36925=CARTESIAN_POINT ( 'NONE',  ( 34.92499999999998295, 22.22500000000000142, 4.500000000000000888 ) ) ;
#36927=ORIENTED_EDGE ( 'NONE', *, *, #101358, .F. ) ;
#36928=VECTOR ( 'NONE', #50187, 999.9999999999998863 ) ;
#36929=CARTESIAN_POINT ( 'NONE',  ( 29.67183060077626777, 11.25929247661560595, 4.000000000000000000 ) ) ;
#36931=DIRECTION ( 'NONE',  ( 0.7071067811865487940, 0.7071067811865463515, 0.000000000000000000 ) ) ;
#36932=AXIS2_PLACEMENT_3D ( 'NONE', #51549, #8000, #60295 ) ;
#36933=CARTESIAN_POINT ( 'NONE',  ( 5.293207492759216315, 20.25929247661550647, 20.83292124670813550 ) ) ;
#36934=LINE ( 'NONE', #115894, #23408 ) ;
#36935=VECTOR ( 'NONE', #66754, 1000.000000000000000 ) ;
#36938=VECTOR ( 'NONE', #3224, 999.9999999999998863 ) ;
#36939=DIRECTION ( 'NONE',  ( 0.7071067811865486830, -0.7071067811865464625, -0.000000000000000000 ) ) ;
#36940=CARTESIAN_POINT ( 'NONE',  ( 24.79996877983148096, 8.259292476615630818, 16.85664084051835232 ) ) ;
#36941=PLANE ( 'NONE',  #52341 ) ;
#36942=DIRECTION ( 'NONE',  ( 0.7071067811865487940, 0.7071067811865463515, -0.000000000000000000 ) ) ;
#36943=DIRECTION ( 'NONE',  ( -0.7071067811865486830, -0.7071067811865464625, 0.000000000000000000 ) ) ;
#36944=VERTEX_POINT ( 'NONE', #135846 ) ;
#36945=ORIENTED_EDGE ( 'NONE', *, *, #107993, .F. ) ;
#36949=EDGE_CURVE ( 'NONE', #10046, #44215, #114090, .T. ) ;
#36950=CARTESIAN_POINT ( 'NONE',  ( -27.29974487139158512, -27.71228299555225405, 4.000000000000000000 ) ) ;
#36951=VECTOR ( 'NONE', #19966, 1000.000000000000227 ) ;
#36952=CARTESIAN_POINT ( 'NONE',  ( -60.48921356237309510, -27.52281430457097500, 5.000000000000000000 ) ) ;
#36953=ORIENTED_EDGE ( 'NONE', *, *, #17744, .F. ) ;
#36955=EDGE_CURVE ( 'NONE', #70831, #44164, #95178, .T. ) ;
#36956=FACE_OUTER_BOUND ( 'NONE', #52832, .T. ) ;
#36959=VERTEX_POINT ( 'NONE', #127843 ) ;
#36960=ORIENTED_EDGE ( 'NONE', *, *, #95698, .F. ) ;
#36961=DIRECTION ( 'NONE',  ( -0.000000000000000000, -0.000000000000000000, 1.000000000000000000 ) ) ;
#36963=CARTESIAN_POINT ( 'NONE',  ( -1.171830600776463838, -5.240707523384232402, 4.000000000000000000 ) ) ;
#36964=ORIENTED_EDGE ( 'NONE', *, *, #30142, .T. ) ;
#36965=VERTEX_POINT ( 'NONE', #137994 ) ;
#36966=ADVANCED_FACE ( 'NONE', ( #71315 ), #16164, .F. ) ;
#36967=ORIENTED_EDGE ( 'NONE', *, *, #75745, .T. ) ;
#36968=CARTESIAN_POINT ( 'NONE',  ( 9.770042794577866729, 21.73644205237998506, 5.000000000000000888 ) ) ;
#36969=EDGE_CURVE ( 'NONE', #13095, #141411, #82211, .T. ) ;
#36970=EDGE_CURVE ( 'NONE', #43634, #110134, #5301, .T. ) ;
#36971=LINE ( 'NONE', #82638, #91742 ) ;
#36973=EDGE_LOOP ( 'NONE', ( #27154, #48549, #116792, #47056 ) ) ;
#36974=CARTESIAN_POINT ( 'NONE',  ( -11.99999999999991296, 11.96639925780213964, 5.000000000000000000 ) ) ;
#36975=ORIENTED_EDGE ( 'NONE', *, *, #91955, .F. ) ;
#36976=ORIENTED_EDGE ( 'NONE', *, *, #84694, .F. ) ;
#36977=EDGE_CURVE ( 'NONE', #118451, #83429, #83634, .T. ) ;
#36978=LINE ( 'NONE', #81234, #51732 ) ;
#36979=FACE_OUTER_BOUND ( 'NONE', #115322, .T. ) ;
#36980=ORIENTED_EDGE ( 'NONE', *, *, #79198, .T. ) ;
#36981=DIRECTION ( 'NONE',  ( -0.7071067811865486830, -0.7071067811865464625, 0.000000000000000000 ) ) ;
#36982=AXIS2_PLACEMENT_3D ( 'NONE', #128803, #49138, #125974 ) ;
#36983=CARTESIAN_POINT ( 'NONE',  ( -23.20666063542136470, 21.75929247661548516, 4.998822639870711626 ) ) ;
#36984=ADVANCED_FACE ( 'NONE', ( #61874 ), #27790, .T. ) ;
#36985=LINE ( 'NONE', #60195, #1982 ) ;
#36986=VECTOR ( 'NONE', #7955, 999.9999999999998863 ) ;
#36988=VECTOR ( 'NONE', #123486, 999.9999999999998863 ) ;
#36990=VECTOR ( 'NONE', #25597, 1000.000000000000000 ) ;
#36991=DIRECTION ( 'NONE',  ( 2.781805975412905890E-17, -0.3543493200069152693, 0.9351131265310292928 ) ) ;
#36992=FACE_BOUND ( 'NONE', #32086, .T. ) ;
#36994=CARTESIAN_POINT ( 'NONE',  ( 5.671830600776432973, 17.25929247661555266, 4.000000000000000000 ) ) ;
#36997=ORIENTED_EDGE ( 'NONE', *, *, #53007, .T. ) ;
#36998=ADVANCED_FACE ( 'NONE', ( #72054 ), #61192, .T. ) ;
#36999=CARTESIAN_POINT ( 'NONE',  ( -23.81601139373100295, 28.73617430169770870, 5.000000000000000000 ) ) ;
#37000=ORIENTED_EDGE ( 'NONE', *, *, #121060, .T. ) ;
#37001=EDGE_CURVE ( 'NONE', #62199, #87041, #104633, .T. ) ;
#37003=AXIS2_PLACEMENT_3D ( 'NONE', #22115, #12668, #44651 ) ;
#37004=ORIENTED_EDGE ( 'NONE', *, *, #28252, .F. ) ;
#37005=ADVANCED_FACE ( 'NONE', ( #49583 ), #40818, .F. ) ;
#37007=ORIENTED_EDGE ( 'NONE', *, *, #29657, .T. ) ;
#37008=VECTOR ( 'NONE', #82541, 999.9999999999998863 ) ;
#37010=DIRECTION ( 'NONE',  ( -0.7071067811865486830, -0.7071067811865464625, 0.000000000000000000 ) ) ;
#37012=CARTESIAN_POINT ( 'NONE',  ( -41.99451991528749062, 28.92564299267967343, 4.000000000000000000 ) ) ;
#37014=ORIENTED_EDGE ( 'NONE', *, *, #110949, .T. ) ;
#37017=VECTOR ( 'NONE', #89343, 1000.000000000000227 ) ;
#37018=VECTOR ( 'NONE', #109326, 1000.000000000000000 ) ;
#37019=FACE_OUTER_BOUND ( 'NONE', #19298, .T. ) ;
#37021=CARTESIAN_POINT ( 'NONE',  ( 59.99451991528749772, 28.92564299267980132, 4.000000000000000000 ) ) ;
#37022=PLANE ( 'NONE',  #6882 ) ;
#37024=LINE ( 'NONE', #81272, #47087 ) ;
#37025=EDGE_LOOP ( 'NONE', ( #12878, #10621, #100805, #104360 ) ) ;
#37026=ORIENTED_EDGE ( 'NONE', *, *, #24647, .F. ) ;
#37027=ORIENTED_EDGE ( 'NONE', *, *, #113275, .T. ) ;
#37029=DIRECTION ( 'NONE',  ( -0.000000000000000000, 0.3543493200069153248, 0.9351131265310292928 ) ) ;
#37030=VERTEX_POINT ( 'NONE', #103895 ) ;
#37032=ORIENTED_EDGE ( 'NONE', *, *, #119297, .F. ) ;
#37033=PLANE ( 'NONE',  #72266 ) ;
#37034=DIRECTION ( 'NONE',  ( -0.6830127018922181881, 0.6830127018922202975, -0.2588190451025214056 ) ) ;
#37035=VECTOR ( 'NONE', #135417, 1000.000000000000227 ) ;
#37037=VERTEX_POINT ( 'NONE', #82905 ) ;
#37038=VECTOR ( 'NONE', #18191, 1000.000000000000000 ) ;
#37039=CARTESIAN_POINT ( 'NONE',  ( 57.48921356237308800, -27.52281430457095368, 5.000000000000000000 ) ) ;
#37040=VERTEX_POINT ( 'NONE', #139451 ) ;
#37041=CARTESIAN_POINT ( 'NONE',  ( -29.20710678118634007, 9.759292476615621936, 5.000000000000000000 ) ) ;
#37043=VECTOR ( 'NONE', #120594, 1000.000000000000000 ) ;
#37051=DIRECTION ( 'NONE',  ( 0.7071067811865487940, 0.7071067811865463515, 0.000000000000000000 ) ) ;
#37052=AXIS2_PLACEMENT_3D ( 'NONE', #69959, #69212, #124287 ) ;
#37053=ORIENTED_EDGE ( 'NONE', *, *, #95395, .T. ) ;
#37054=DIRECTION ( 'NONE',  ( 0.7071067811865487940, 0.7071067811865463515, -0.000000000000000000 ) ) ;
#37055=DIRECTION ( 'NONE',  ( -0.7071067811865487940, 0.7071067811865463515, 0.000000000000000000 ) ) ;
#37056=CARTESIAN_POINT ( 'NONE',  ( 26.99999999999981171, -21.84840872380821963, 2.849755605029670846 ) ) ;
#37058=VERTEX_POINT ( 'NONE', #5997 ) ;
#37059=CARTESIAN_POINT ( 'NONE',  ( 20.29387692260790743, 22.22500000000000142, 4.000000000000000000 ) ) ;
#37060=CARTESIAN_POINT ( 'NONE',  ( -34.49999999999975842, -8.568876922607724822, 4.000000000000000000 ) ) ;
#37061=LINE ( 'NONE', #26903, #67733 ) ;
#37062=ORIENTED_EDGE ( 'NONE', *, *, #67562, .F. ) ;
#37063=DIRECTION ( 'NONE',  ( 0.7071067811865487940, 0.7071067811865463515, 0.000000000000000000 ) ) ;
#37064=VECTOR ( 'NONE', #53068, 999.9999999999998863 ) ;
#37065=DIRECTION ( 'NONE',  ( -0.3543493200069162685, -0.000000000000000000, -0.9351131265310288487 ) ) ;
#37066=ORIENTED_EDGE ( 'NONE', *, *, #133855, .T. ) ;
#37067=ADVANCED_FACE ( 'NONE', ( #40137 ), #50273, .F. ) ;
#37068=CARTESIAN_POINT ( 'NONE',  ( 26.20710678118636494, 12.75929247661558996, 5.000000000000000000 ) ) ;
#37069=ORIENTED_EDGE ( 'NONE', *, *, #12717, .F. ) ;
#37070=EDGE_CURVE ( 'NONE', #72412, #135854, #29917, .T. ) ;
#37072=CARTESIAN_POINT ( 'NONE',  ( 18.48921356237309510, -27.52281430457068367, 5.000000000000000000 ) ) ;
#37073=AXIS2_PLACEMENT_3D ( 'NONE', #75110, #119279, #86686 ) ;
#37074=ORIENTED_EDGE ( 'NONE', *, *, #140727, .F. ) ;
#37077=LINE ( 'NONE', #49424, #89184 ) ;
#37078=DIRECTION ( 'NONE',  ( -0.6830127018922181881, 0.6830127018922202975, -0.2588190451025214056 ) ) ;
#37079=EDGE_LOOP ( 'NONE', ( #62720, #81116, #19623, #131902 ) ) ;
#37080=ADVANCED_FACE ( 'NONE', ( #116936 ), #50985, .F. ) ;
#37081=PLANE ( 'NONE',  #87850 ) ;
#37083=CARTESIAN_POINT ( 'NONE',  ( -84.18398860626899705, 28.73617430169846187, 5.000000000000000000 ) ) ;
#37084=CARTESIAN_POINT ( 'NONE',  ( 0.000000000000000000, 0.000000000000000000, 5.000000000000000000 ) ) ;
#37087=LINE ( 'NONE', #14630, #100986 ) ;
#37088=ORIENTED_EDGE ( 'NONE', *, *, #138060, .T. ) ;
#37089=EDGE_CURVE ( 'NONE', #59942, #51133, #95898, .T. ) ;
#37090=ORIENTED_EDGE ( 'NONE', *, *, #33250, .T. ) ;
#37094=ORIENTED_EDGE ( 'NONE', *, *, #113549, .T. ) ;
#37096=EDGE_LOOP ( 'NONE', ( #118959, #142014, #82402, #100003 ) ) ;
#37097=VECTOR ( 'NONE', #13948, 1000.000000000000000 ) ;
#37098=CARTESIAN_POINT ( 'NONE',  ( -23.72174548431413044, 8.259292476615634371, 11.78515199841145034 ) ) ;
#37099=VECTOR ( 'NONE', #57229, 1000.000000000000000 ) ;
#37100=EDGE_CURVE ( 'NONE', #19920, #138101, #15445, .T. ) ;
#37101=VECTOR ( 'NONE', #58165, 1000.000000000000227 ) ;
#37104=VECTOR ( 'NONE', #53434, 1000.000000000000000 ) ;
#37106=CARTESIAN_POINT ( 'NONE',  ( 17.67183060077634948, -9.740707523384180888, 4.000000000000000000 ) ) ;
#37108=VERTEX_POINT ( 'NONE', #87882 ) ;
#37109=PLANE ( 'NONE',  #62715 ) ;
#37110=CARTESIAN_POINT ( 'NONE',  ( -15.32816939922342137, 17.25929247661553489, 4.000000000000000000 ) ) ;
#37112=VECTOR ( 'NONE', #102924, 1000.000000000000000 ) ;
#37114=CARTESIAN_POINT ( 'NONE',  ( 47.99451991528749062, 28.92564299267971251, 4.000000000000000000 ) ) ;
#37115=DIRECTION ( 'NONE',  ( 1.000000000000000000, 0.000000000000000000, 0.000000000000000000 ) ) ;
#37116=FACE_OUTER_BOUND ( 'NONE', #92996, .T. ) ;
#37118=PLANE ( 'NONE',  #18916 ) ;
#37119=FACE_OUTER_BOUND ( 'NONE', #114533, .T. ) ;
#37120=EDGE_LOOP ( 'NONE', ( #45437, #129677, #70879, #70349, #55405 ) ) ;
#37121=VERTEX_POINT ( 'NONE', #129968 ) ;
#37123=EDGE_LOOP ( 'NONE', ( #102101, #62154, #134795, #140801 ) ) ;
#37124=ORIENTED_EDGE ( 'NONE', *, *, #68395, .T. ) ;
#37125=FACE_OUTER_BOUND ( 'NONE', #57718, .T. ) ;
#37126=EDGE_CURVE ( 'NONE', #87956, #64810, #107487, .T. ) ;
#37128=FACE_OUTER_BOUND ( 'NONE', #114268, .T. ) ;
#37129=ORIENTED_EDGE ( 'NONE', *, *, #101009, .T. ) ;
#37131=CARTESIAN_POINT ( 'NONE',  ( -24.29974487139158867, -27.71228299555223273, 4.000000000000000000 ) ) ;
#37133=EDGE_CURVE ( 'NONE', #68247, #83424, #19763, .T. ) ;
#37134=CARTESIAN_POINT ( 'NONE',  ( 24.29974487139158867, -27.71228299555223273, 4.000000000000000000 ) ) ;
#37135=VECTOR ( 'NONE', #85986, 1000.000000000000000 ) ;
#37136=VECTOR ( 'NONE', #98694, 1000.000000000000000 ) ;
#37138=VERTEX_POINT ( 'NONE', #52390 ) ;
#37139=VECTOR ( 'NONE', #46796, 999.9999999999998863 ) ;
#37140=CARTESIAN_POINT ( 'NONE',  ( -36.48921356237310221, -27.52281430457080802, 5.000000000000000000 ) ) ;
#37141=VERTEX_POINT ( 'NONE', #132123 ) ;
#37143=VECTOR ( 'NONE', #121410, 1000.000000000000000 ) ;
#37144=EDGE_CURVE ( 'NONE', #122865, #13632, #77037, .T. ) ;
#37148=VERTEX_POINT ( 'NONE', #140814 ) ;
#37150=VERTEX_POINT ( 'NONE', #85728 ) ;
#37151=AXIS2_PLACEMENT_3D ( 'NONE', #11349, #53475, #86827 ) ;
#37152=CARTESIAN_POINT ( 'NONE',  ( 15.18398860626900237, 28.73617430169797871, 5.000000000000000000 ) ) ;
#37153=ADVANCED_FACE ( 'NONE', ( #119071 ), #97292, .F. ) ;
#37154=DIRECTION ( 'NONE',  ( -0.7071067811865486830, -0.7071067811865464625, 0.000000000000000000 ) ) ;
#37155=CARTESIAN_POINT ( 'NONE',  ( -6.793339364578430128, 21.75929247661548871, 4.998822639870703632 ) ) ;
#37156=EDGE_CURVE ( 'NONE', #33217, #59038, #44414, .T. ) ;
#37157=VECTOR ( 'NONE', #88090, 1000.000000000000000 ) ;
#37158=EDGE_CURVE ( 'NONE', #84039, #139138, #55265, .T. ) ;
#37162=ORIENTED_EDGE ( 'NONE', *, *, #92943, .T. ) ;
#37164=VECTOR ( 'NONE', #4979, 999.9999999999998863 ) ;
#37165=CARTESIAN_POINT ( 'NONE',  ( 34.92499999999998295, 14.19452376399133442, 8.043047640789311004 ) ) ;
#37166=ADVANCED_FACE ( 'NONE', ( #120467 ), #121212, .F. ) ;
#37167=ORIENTED_EDGE ( 'NONE', *, *, #21580, .T. ) ;
#37168=FACE_OUTER_BOUND ( 'NONE', #22047, .T. ) ;
#37169=EDGE_LOOP ( 'NONE', ( #129195, #47106, #13212, #86086 ) ) ;
#37170=CARTESIAN_POINT ( 'NONE',  ( -28.17183060077627488, 3.759292476615683665, 4.000000000000000000 ) ) ;
#37173=DIRECTION ( 'NONE',  ( 0.7071067811865486830, -0.7071067811865464625, -0.000000000000000000 ) ) ;
#37174=FACE_BOUND ( 'NONE', #49938, .T. ) ;
#37175=DIRECTION ( 'NONE',  ( 0.7071067811865487940, 0.7071067811865463515, -0.000000000000000000 ) ) ;
#37176=LINE ( 'NONE', #92251, #65273 ) ;
#37177=CARTESIAN_POINT ( 'NONE',  ( 30.29974487139158867, -27.71228299555227537, 4.000000000000000000 ) ) ;
#37179=DIRECTION ( 'NONE',  ( -0.7071067811865486830, -0.7071067811865464625, -0.000000000000000000 ) ) ;
#37180=ORIENTED_EDGE ( 'NONE', *, *, #9833, .F. ) ;
#37181=AXIS2_PLACEMENT_3D ( 'NONE', #16782, #82770, #102394 ) ;
#37183=DIRECTION ( 'NONE',  ( -0.7071067811865486830, -0.7071067811865464625, 0.000000000000000000 ) ) ;
#37184=VERTEX_POINT ( 'NONE', #86473 ) ;
#37186=EDGE_CURVE ( 'NONE', #94430, #118518, #53090, .T. ) ;
#37187=ORIENTED_EDGE ( 'NONE', *, *, #51509, .F. ) ;
#37190=CARTESIAN_POINT ( 'NONE',  ( -2.510786437626908008, -27.52281430457053446, 5.000000000000000000 ) ) ;
#37191=CARTESIAN_POINT ( 'NONE',  ( 2.999999999999981792, -19.06887692260762179, 4.000000000000000000 ) ) ;
#37192=ORIENTED_EDGE ( 'NONE', *, *, #39102, .T. ) ;
#37194=VECTOR ( 'NONE', #66800, 999.9999999999998863 ) ;
#37195=ADVANCED_FACE ( 'NONE', ( #9580 ), #53853, .F. ) ;
#37197=AXIS2_PLACEMENT_3D ( 'NONE', #51797, #73542, #107571 ) ;
#37198=DIRECTION ( 'NONE',  ( -0.7071067811865487940, 0.7071067811865463515, -0.000000000000000000 ) ) ;
#37199=CARTESIAN_POINT ( 'NONE',  ( -15.29974487139158867, -27.71228299555216879, 4.000000000000000000 ) ) ;
#37200=CARTESIAN_POINT ( 'NONE',  ( -26.01088028653930451, -22.02621442084248216, 4.990779571109225543 ) ) ;
#37201=CARTESIAN_POINT ( 'NONE',  ( -21.48921356237309155, -27.52281430457070499, 5.000000000000000000 ) ) ;
#37202=FACE_OUTER_BOUND ( 'NONE', #47631, .T. ) ;
#37204=VECTOR ( 'NONE', #114610, 1000.000000000000000 ) ;
#37205=AXIS2_PLACEMENT_3D ( 'NONE', #510, #131774, #76700 ) ;
#37207=ORIENTED_EDGE ( 'NONE', *, *, #101118, .T. ) ;
#37208=AXIS2_PLACEMENT_3D ( 'NONE', #56205, #5897, #105247 ) ;
#37209=DIRECTION ( 'NONE',  ( -0.6830127018922180770, -0.6830127018922204085, -0.2588190451025213501 ) ) ;
#37210=CARTESIAN_POINT ( 'NONE',  ( 5.999999999999960032, 10.55218569542906160, 5.000000000000000000 ) ) ;
#37211=ORIENTED_EDGE ( 'NONE', *, *, #121943, .F. ) ;
#37212=ORIENTED_EDGE ( 'NONE', *, *, #44357, .T. ) ;
#37213=EDGE_LOOP ( 'NONE', ( #51935, #25685, #24876, #99439 ) ) ;
#37214=CARTESIAN_POINT ( 'NONE',  ( 11.99999999999991651, -16.06887692260765377, 4.000000000000000000 ) ) ;
#37215=ORIENTED_EDGE ( 'NONE', *, *, #115762, .T. ) ;
#37216=VECTOR ( 'NONE', #83136, 1000.000000000000000 ) ;
#37217=CARTESIAN_POINT ( 'NONE',  ( -2.206660635421508143, 21.75929247661549937, 4.998822639870708073 ) ) ;
#37220=DIRECTION ( 'NONE',  ( 0.7071067811865487940, 0.7071067811865463515, 0.000000000000000000 ) ) ;
#37221=VERTEX_POINT ( 'NONE', #131395 ) ;
#37223=DIRECTION ( 'NONE',  ( 0.7071067811865487940, -0.7071067811865463515, 0.000000000000000000 ) ) ;
#37224=LINE ( 'NONE', #113337, #85950 ) ;
#37225=EDGE_CURVE ( 'NONE', #95580, #58969, #32076, .T. ) ;
#37226=EDGE_CURVE ( 'NONE', #78422, #86060, #98742, .T. ) ;
#37228=LINE ( 'NONE', #115456, #8126 ) ;
#37230=VERTEX_POINT ( 'NONE', #142969 ) ;
#37231=ORIENTED_EDGE ( 'NONE', *, *, #52803, .F. ) ;
#37232=DIRECTION ( 'NONE',  ( 0.7071067811865487940, 0.7071067811865463515, 0.000000000000000000 ) ) ;
#37233=CARTESIAN_POINT ( 'NONE',  ( -20.52663903635772513, -5.240707523384225297, 16.25846745537490889 ) ) ;
#37234=PLANE ( 'NONE',  #135062 ) ;
#37235=ORIENTED_EDGE ( 'NONE', *, *, #102896, .F. ) ;
#37236=AXIS2_PLACEMENT_3D ( 'NONE', #46302, #3441, #91897 ) ;
#37237=CARTESIAN_POINT ( 'NONE',  ( -1.019877749285469370, -17.24070752338410273, 20.23474786156469207 ) ) ;
#37238=LINE ( 'NONE', #79367, #142823 ) ;
#37240=AXIS2_PLACEMENT_3D ( 'NONE', #55141, #44280, #77620 ) ;
#37241=LINE ( 'NONE', #37974, #19360 ) ;
#37242=LINE ( 'NONE', #116227, #21049 ) ;
#37243=CARTESIAN_POINT ( 'NONE',  ( 81.29974487139159578, -27.71228299555262709, 4.000000000000000000 ) ) ;
#37244=ORIENTED_EDGE ( 'NONE', *, *, #28073, .F. ) ;
#37245=LINE ( 'NONE', #56892, #73976 ) ;
#37246=VECTOR ( 'NONE', #7292, 1000.000000000000000 ) ;
#37247=LINE ( 'NONE', #36530, #130380 ) ;
#37248=CARTESIAN_POINT ( 'NONE',  ( 63.18398860626900415, 28.73617430169831621, 5.000000000000000000 ) ) ;
#37249=EDGE_CURVE ( 'NONE', #107457, #117579, #43663, .T. ) ;
#37250=DIRECTION ( 'NONE',  ( -0.000000000000000000, -0.3543493200069152693, 0.9351131265310292928 ) ) ;
#37252=EDGE_CURVE ( 'NONE', #18669, #136089, #4188, .T. ) ;
#37254=AXIS2_PLACEMENT_3D ( 'NONE', #83654, #28543, #72801 ) ;
#37256=CARTESIAN_POINT ( 'NONE',  ( -34.92500000000001137, -15.18334561358941315, 4.500000000000000888 ) ) ;
#37258=EDGE_CURVE ( 'NONE', #73784, #82859, #113009, .T. ) ;
#37259=ADVANCED_FACE ( 'NONE', ( #69551 ), #60830, .F. ) ;
#37262=AXIS2_PLACEMENT_3D ( 'NONE', #47732, #4843, #49855 ) ;
#37263=DIRECTION ( 'NONE',  ( 0.7071067811865486830, -0.7071067811865464625, -0.000000000000000000 ) ) ;
#37264=CARTESIAN_POINT ( 'NONE',  ( 20.99999999999985079, 10.93112307739207267, 4.000000000000000000 ) ) ;
#37265=CARTESIAN_POINT ( 'NONE',  ( -9.643187427517323940, -20.24070752338407075, 21.22881796311210323 ) ) ;
#37266=ORIENTED_EDGE ( 'NONE', *, *, #112583, .T. ) ;
#37267=EDGE_CURVE ( 'NONE', #56327, #137982, #70289, .T. ) ;
#37268=DIRECTION ( 'NONE',  ( 0.7071067811865486830, -0.7071067811865464625, -0.000000000000000000 ) ) ;
#37269=VECTOR ( 'NONE', #56433, 1000.000000000000227 ) ;
#37270=CARTESIAN_POINT ( 'NONE',  ( 11.67183060077639389, -21.74070752338406365, 4.000000000000000000 ) ) ;
#37271=VECTOR ( 'NONE', #91983, 1000.000000000000000 ) ;
#37272=PLANE ( 'NONE',  #50530 ) ;
#37274=CARTESIAN_POINT ( 'NONE',  ( -0.7816268829249449768, 21.74787736706806029, 4.999607392498049308 ) ) ;
#37275=ADVANCED_FACE ( 'NONE', ( #126729 ), #70967, .F. ) ;
#37276=ORIENTED_EDGE ( 'NONE', *, *, #13043, .T. ) ;
#37277=DIRECTION ( 'NONE',  ( -0.6830127018922180770, -0.6830127018922204085, -0.2588190451025213501 ) ) ;
#37278=EDGE_LOOP ( 'NONE', ( #49187, #63202, #31434, #82938 ) ) ;
#37279=LINE ( 'NONE', #96426, #113695 ) ;
#37281=AXIS2_PLACEMENT_3D ( 'NONE', #46188, #137454, #91110 ) ;
#37282=LINE ( 'NONE', #79409, #61738 ) ;
#37283=EDGE_CURVE ( 'NONE', #71611, #91617, #92677, .T. ) ;
#37284=CARTESIAN_POINT ( 'NONE',  ( 33.79289321881321939, -20.24070752338407786, 5.000000000000000000 ) ) ;
#37285=CARTESIAN_POINT ( 'NONE',  ( -36.29974487139159578, -27.71228299555231445, 4.000000000000000000 ) ) ;
#37286=DIRECTION ( 'NONE',  ( 0.3543493200069162685, -0.000000000000000000, -0.9351131265310288487 ) ) ;
#37287=CARTESIAN_POINT ( 'NONE',  ( 23.99999999999984368, 14.58746187583909837, 4.000000000000000000 ) ) ;
#37289=ORIENTED_EDGE ( 'NONE', *, *, #58843, .F. ) ;
#37290=FACE_OUTER_BOUND ( 'NONE', #26842, .T. ) ;
#37292=EDGE_CURVE ( 'NONE', #56990, #82053, #104991, .T. ) ;
#37293=VECTOR ( 'NONE', #8709, 1000.000000000000000 ) ;
#37294=CARTESIAN_POINT ( 'NONE',  ( -34.92500000000001137, 22.22500000000000142, 4.000000000000000000 ) ) ;
#37297=LINE ( 'NONE', #125749, #78542 ) ;
#37298=VERTEX_POINT ( 'NONE', #49928 ) ;
#37299=ORIENTED_EDGE ( 'NONE', *, *, #553, .T. ) ;
#37301=DIRECTION ( 'NONE',  ( 0.7071067811865487940, -0.7071067811865463515, 0.000000000000000000 ) ) ;
#37302=CARTESIAN_POINT ( 'NONE',  ( 30.48921356237309510, -27.52281430457076894, 5.000000000000000000 ) ) ;
#37303=LINE ( 'NONE', #5357, #96003 ) ;
#37304=EDGE_CURVE ( 'NONE', #43201, #94183, #115122, .T. ) ;
#37305=ORIENTED_EDGE ( 'NONE', *, *, #8588, .T. ) ;
#37306=( BOUNDED_CURVE ( )  B_SPLINE_CURVE ( 3, ( #123660, #122920, #57692, #101870 ),
 .UNSPECIFIED., .F., .F. ) 
 B_SPLINE_CURVE_WITH_KNOTS ( ( 4, 4 ),
 ( 1.208578181583237932, 1.359146454359414724 ),
 .UNSPECIFIED. ) 
 CURVE ( )  GEOMETRIC_REPRESENTATION_ITEM ( )  RATIONAL_B_SPLINE_CURVE ( ( 1.000000000000000000, 0.9981116584018959736, 0.9981116584018959736, 1.000000000000000000 ) ) 
 REPRESENTATION_ITEM ( '' )  );
#37307=CARTESIAN_POINT ( 'NONE',  ( -12.70701326429296252, -21.74070752338406010, 4.999753212805220670 ) ) ;
#37308=VECTOR ( 'NONE', #48252, 1000.000000000000000 ) ;
#37309=EDGE_CURVE ( 'NONE', #75424, #113572, #94107, .T. ) ;
#37310=VECTOR ( 'NONE', #89068, 1000.000000000000000 ) ;
#37311=CARTESIAN_POINT ( 'NONE',  ( 39.29974487139159578, -27.71228299555233576, 4.000000000000000000 ) ) ;
#37313=EDGE_CURVE ( 'NONE', #42725, #101750, #113738, .T. ) ;
#37314=DIRECTION ( 'NONE',  ( -0.7071067811865486830, -0.7071067811865464625, 0.000000000000000000 ) ) ;
#37315=VERTEX_POINT ( 'NONE', #25287 ) ;
#37316=AXIS2_PLACEMENT_3D ( 'NONE', #102170, #81134, #49227 ) ;
#37317=ORIENTED_EDGE ( 'NONE', *, *, #102549, .F. ) ;
#37318=VECTOR ( 'NONE', #54768, 1000.000000000000000 ) ;
#37320=AXIS2_PLACEMENT_3D ( 'NONE', #26800, #82615, #115193 ) ;
#37321=DIRECTION ( 'NONE',  ( -0.7071067811865487940, 0.7071067811865463515, 0.000000000000000000 ) ) ;
#37323=AXIS2_PLACEMENT_3D ( 'NONE', #94446, #16903, #129213 ) ;
#37325=CARTESIAN_POINT ( 'NONE',  ( 32.99999999999977263, -21.84840872380821608, 2.849755605029683281 ) ) ;
#37326=DIRECTION ( 'NONE',  ( -0.7071067811865486830, 0.7071067811865464625, 0.000000000000000000 ) ) ;
#37327=CARTESIAN_POINT ( 'NONE',  ( -30.18398860626900060, 28.73617430169808173, 5.000000000000000000 ) ) ;
#37328=CARTESIAN_POINT ( 'NONE',  ( 8.161706124526148187, -6.740707523384205757, 16.75550250614869086 ) ) ;
#37329=VERTEX_POINT ( 'NONE', #15793 ) ;
#37330=DIRECTION ( 'NONE',  ( -0.000000000000000000, 0.3543493200069153248, 0.9351131265310292928 ) ) ;
#37331=DIRECTION ( 'NONE',  ( 0.3543493200069162685, -0.000000000000000000, -0.9351131265310288487 ) ) ;
#37334=FACE_OUTER_BOUND ( 'NONE', #12220, .T. ) ;
#37335=ORIENTED_EDGE ( 'NONE', *, *, #111004, .T. ) ;
#37336=ORIENTED_EDGE ( 'NONE', *, *, #35430, .F. ) ;
#37337=VECTOR ( 'NONE', #129694, 1000.000000000000000 ) ;
#37338=ADVANCED_FACE ( 'NONE', ( #102168 ), #59391, .F. ) ;
#37339=CYLINDRICAL_SURFACE ( 'NONE', #73051, 0.5000000000000004441 ) ;
#37340=CARTESIAN_POINT ( 'NONE',  ( -11.99999999999992006, -22.06887692260758982, 4.000000000000000000 ) ) ;
#37341=DIRECTION ( 'NONE',  ( -0.7071067811865487940, 0.7071067811865463515, -0.000000000000000000 ) ) ;
#37342=DIRECTION ( 'NONE',  ( 0.7071067811865487940, -0.7071067811865463515, 0.000000000000000000 ) ) ;
#37343=ORIENTED_EDGE ( 'NONE', *, *, #29800, .T. ) ;
#37344=ORIENTED_EDGE ( 'NONE', *, *, #4713, .T. ) ;
#37345=DIRECTION ( 'NONE',  ( 1.000000000000000000, 0.000000000000000000, 0.000000000000000000 ) ) ;
#37347=EDGE_CURVE ( 'NONE', #34296, #47990, #38326, .T. ) ;
#37348=VECTOR ( 'NONE', #12555, 1000.000000000000000 ) ;
#37349=ORIENTED_EDGE ( 'NONE', *, *, #13743, .T. ) ;
#37350=VECTOR ( 'NONE', #10731, 1000.000000000000000 ) ;
#37351=DIRECTION ( 'NONE',  ( -0.7071067811865486830, 0.7071067811865464625, 0.000000000000000000 ) ) ;
#37352=ORIENTED_EDGE ( 'NONE', *, *, #63525, .T. ) ;
#37353=AXIS2_PLACEMENT_3D ( 'NONE', #30244, #74496, #107786 ) ;
#37354=LINE ( 'NONE', #26470, #89584 ) ;
#37355=LINE ( 'NONE', #125058, #3004 ) ;
#37357=FACE_BOUND ( 'NONE', #20405, .T. ) ;
#37358=VECTOR ( 'NONE', #34083, 1000.000000000000227 ) ;
#37359=DIRECTION ( 'NONE',  ( -0.6830127018922181881, 0.6830127018922202975, -0.2588190451025214056 ) ) ;
#37360=DIRECTION ( 'NONE',  ( -1.000000000000000000, 0.000000000000000000, -0.000000000000000000 ) ) ;
#37362=CARTESIAN_POINT ( 'NONE',  ( -31.49999999999977973, 1.466399257802248446, 5.000000000000000000 ) ) ;
#37364=EDGE_LOOP ( 'NONE', ( #105220, #31047, #1079, #95387 ) ) ;
#37365=EDGE_CURVE ( 'NONE', #46917, #56980, #115837, .T. ) ;
#37366=VECTOR ( 'NONE', #32843, 1000.000000000000227 ) ;
#37367=ORIENTED_EDGE ( 'NONE', *, *, #52673, .T. ) ;
#37369=ORIENTED_EDGE ( 'NONE', *, *, #138625, .F. ) ;
#37370=DIRECTION ( 'NONE',  ( -0.7071067811865486830, 0.7071067811865464625, 0.000000000000000000 ) ) ;
#37371=VECTOR ( 'NONE', #73355, 1000.000000000000000 ) ;
#37372=CARTESIAN_POINT ( 'NONE',  ( -59.99451991528749772, 28.92564299267980132, 4.000000000000000000 ) ) ;
#37374=LINE ( 'NONE', #73573, #117378 ) ;
#37375=LINE ( 'NONE', #72184, #105010 ) ;
#37379=DIRECTION ( 'NONE',  ( -0.6830127018922180770, -0.6830127018922204085, -0.2588190451025213501 ) ) ;
#37380=CARTESIAN_POINT ( 'NONE',  ( 1.734723475976807094E-15, 2.966399257802227130, 5.000000000000000000 ) ) ;
#37381=DIRECTION ( 'NONE',  ( -0.3543493200069162685, -0.000000000000000000, -0.9351131265310288487 ) ) ;
#37383=AXIS2_PLACEMENT_3D ( 'NONE', #109462, #134081, #23130 ) ;
#37384=CARTESIAN_POINT ( 'NONE',  ( 29.68342038867192656, -6.740707523384212863, 11.88629033278117575 ) ) ;
#37385=ORIENTED_EDGE ( 'NONE', *, *, #122350, .T. ) ;
#37386=DIRECTION ( 'NONE',  ( -0.000000000000000000, -0.3543493200069152693, 0.9351131265310292928 ) ) ;
#37387=CARTESIAN_POINT ( 'NONE',  ( 22.17183060077631751, -2.240707523384257716, 4.000000000000000000 ) ) ;
#37388=VERTEX_POINT ( 'NONE', #125337 ) ;
#37389=EDGE_LOOP ( 'NONE', ( #117903, #122809, #40661, #10884 ) ) ;
#37390=VERTEX_POINT ( 'NONE', #66854 ) ;
#37397=LINE ( 'NONE', #123717, #135888 ) ;
#37398=ORIENTED_EDGE ( 'NONE', *, *, #36378, .F. ) ;
#37399=CARTESIAN_POINT ( 'NONE',  ( -6.005480084712508493, 28.92564299267933947, 4.000000000000000000 ) ) ;
#37400=CARTESIAN_POINT ( 'NONE',  ( -34.92500000000001137, -22.22500000000000142, 4.500000000000000888 ) ) ;
#37401=VECTOR ( 'NONE', #55620, 1000.000000000000000 ) ;
#37402=LINE ( 'NONE', #80222, #766 ) ;
#37403=ORIENTED_EDGE ( 'NONE', *, *, #84518, .F. ) ;
#37404=ORIENTED_EDGE ( 'NONE', *, *, #12373, .F. ) ;
#37406=CARTESIAN_POINT ( 'NONE',  ( 38.16170612452596345, -6.740707523384209310, 16.75550250614876546 ) ) ;
#37408=VECTOR ( 'NONE', #45406, 1000.000000000000000 ) ;
#37409=VERTEX_POINT ( 'NONE', #48476 ) ;
#37410=CARTESIAN_POINT ( 'NONE',  ( -36.18398860626899705, 28.73617430169812437, 5.000000000000000000 ) ) ;
#37411=VERTEX_POINT ( 'NONE', #13679 ) ;
#37412=EDGE_LOOP ( 'NONE', ( #70072, #99344, #131097, #29380 ) ) ;
#37413=EDGE_LOOP ( 'NONE', ( #49343, #31559, #21832, #21498 ) ) ;
#37414=ORIENTED_EDGE ( 'NONE', *, *, #803, .F. ) ;
#37415=ADVANCED_FACE ( 'NONE', ( #57971 ), #47118, .F. ) ;
#37417=VECTOR ( 'NONE', #85939, 999.9999999999998863 ) ;
#37419=AXIS2_PLACEMENT_3D ( 'NONE', #121591, #45510, #13531 ) ;
#37423=CARTESIAN_POINT ( 'NONE',  ( 22.17183060077631396, 9.759292476615614831, 4.000000000000000000 ) ) ;
#37424=DIRECTION ( 'NONE',  ( -0.3543493200069162685, -0.000000000000000000, -0.9351131265310288487 ) ) ;
#37425=EDGE_CURVE ( 'NONE', #80458, #33564, #3514, .T. ) ;
#37426=EDGE_CURVE ( 'NONE', #108226, #62844, #117972, .T. ) ;
#37427=CARTESIAN_POINT ( 'NONE',  ( 27.32816939922333432, 2.259292476615690770, 4.000000000000000000 ) ) ;
#37429=ORIENTED_EDGE ( 'NONE', *, *, #71520, .F. ) ;
#37431=ADVANCED_FACE ( 'NONE', ( #41895 ), #28161, .F. ) ;
#37435=EDGE_CURVE ( 'NONE', #73261, #114456, #140472, .T. ) ;
#37437=CARTESIAN_POINT ( 'NONE',  ( -5.282422613574296655, -21.73023691814493930, 5.000000000000000888 ) ) ;
#37438=VERTEX_POINT ( 'NONE', #130338 ) ;
#37439=ORIENTED_EDGE ( 'NONE', *, *, #18103, .T. ) ;
#37440=EDGE_CURVE ( 'NONE', #49004, #9326, #51349, .T. ) ;
#37442=LINE ( 'NONE', #70110, #74201 ) ;
#37443=CARTESIAN_POINT ( 'NONE',  ( 23.51078643762690490, -27.52281430457038880, 5.000000000000000000 ) ) ;
#37445=CARTESIAN_POINT ( 'NONE',  ( -22.49999999999984723, 18.43112307739199807, 4.000000000000000000 ) ) ;
#37446=ADVANCED_FACE ( 'NONE', ( #107827 ), #52742, .F. ) ;
#37447=CARTESIAN_POINT ( 'NONE',  ( -24.48921356237309510, -27.52281430457072631, 5.000000000000000000 ) ) ;
#37448=CARTESIAN_POINT ( 'NONE',  ( 34.49999999999975131, 11.52377502935406106, -1.522421517564165550 ) ) ;
#37450=AXIS2_PLACEMENT_3D ( 'NONE', #47226, #91402, #104380 ) ;
#37451=CARTESIAN_POINT ( 'NONE',  ( -69.48921356237309510, -27.52281430457103895, 5.000000000000000000 ) ) ;
#37452=ADVANCED_FACE ( 'NONE', ( #129588 ), #53480, .T. ) ;
#37453=VECTOR ( 'NONE', #74262, 1000.000000000000227 ) ;
#37454=CARTESIAN_POINT ( 'NONE',  ( 11.99999999999992006, 9.631307414974342507, -9.079085613539515265 ) ) ;
#37455=FACE_OUTER_BOUND ( 'NONE', #123234, .T. ) ;
#37456=CARTESIAN_POINT ( 'NONE',  ( -15.32816939922342137, 20.25929247661551358, 4.000000000000000000 ) ) ;
#37458=DIRECTION ( 'NONE',  ( 0.3543493200069162685, -0.000000000000000000, -0.9351131265310288487 ) ) ;
#37460=DIRECTION ( 'NONE',  ( -0.7071067811865486830, 0.7071067811865464625, 0.000000000000000000 ) ) ;
#37461=AXIS2_PLACEMENT_3D ( 'NONE', #126276, #26953, #27661 ) ;
#37462=ORIENTED_EDGE ( 'NONE', *, *, #111628, .F. ) ;
#37463=EDGE_CURVE ( 'NONE', #35947, #116804, #6346, .T. ) ;
#37464=LINE ( 'NONE', #124452, #29783 ) ;
#37465=CARTESIAN_POINT ( 'NONE',  ( -34.45011844616455221, 15.00230414159380565, 5.000000000000000888 ) ) ;
#37466=ORIENTED_EDGE ( 'NONE', *, *, #11749, .F. ) ;
#37467=DIRECTION ( 'NONE',  ( -0.6830127018922181881, 0.6830127018922202975, -0.2588190451025214056 ) ) ;
#37468=DIRECTION ( 'NONE',  ( 0.7071067811865487940, 0.7071067811865463515, 0.000000000000000000 ) ) ;
#37471=FACE_OUTER_BOUND ( 'NONE', #137672, .T. ) ;
#37472=ORIENTED_EDGE ( 'NONE', *, *, #111550, .T. ) ;
#37474=ORIENTED_EDGE ( 'NONE', *, *, #142324, .T. ) ;
#37475=ADVANCED_FACE ( 'NONE', ( #7067 ), #97687, .F. ) ;
#37476=VECTOR ( 'NONE', #62706, 1000.000000000000227 ) ;
#37477=CARTESIAN_POINT ( 'NONE',  ( 39.29974487139159578, -27.71228299555233576, 4.000000000000000000 ) ) ;
#37479=DIRECTION ( 'NONE',  ( -0.7071067811865486830, -0.7071067811865464625, -0.000000000000000000 ) ) ;
#37481=ORIENTED_EDGE ( 'NONE', *, *, #105231, .T. ) ;
#37482=CARTESIAN_POINT ( 'NONE',  ( -12.18398860626900060, 28.73617430169795739, 5.000000000000000000 ) ) ;
#37483=CARTESIAN_POINT ( 'NONE',  ( -28.17183060077627133, 15.75929247661555976, 4.000000000000000000 ) ) ;
#37484=DIRECTION ( 'NONE',  ( -0.000000000000000000, -0.3543493200069152693, 0.9351131265310292928 ) ) ;
#37486=VECTOR ( 'NONE', #11434, 1000.000000000000000 ) ;
#37488=DIRECTION ( 'NONE',  ( 0.6830127018922180770, -0.6830127018922204085, -0.2588190451025213501 ) ) ;
#37489=AXIS2_PLACEMENT_3D ( 'NONE', #5855, #116786, #37827 ) ;
#37490=ORIENTED_EDGE ( 'NONE', *, *, #51785, .T. ) ;
#37491=CARTESIAN_POINT ( 'NONE',  ( -27.48921356237309155, -27.52281430457074762, 5.000000000000000000 ) ) ;
#37495=ADVANCED_FACE ( 'NONE', ( #74537 ), #116589, .T. ) ;
#37496=DIRECTION ( 'NONE',  ( -0.6830127018922181881, 0.6830127018922202975, -0.2588190451025214056 ) ) ;
#37497=CARTESIAN_POINT ( 'NONE',  ( 51.48921356237309510, -27.52281430457091460, 5.000000000000000000 ) ) ;
#37498=CARTESIAN_POINT ( 'NONE',  ( 9.707106781186482181, 14.25929247661557220, 5.000000000000000000 ) ) ;
#37502=CARTESIAN_POINT ( 'NONE',  ( 22.49999999999984723, 18.43112307739199807, 4.000000000000000000 ) ) ;
#37503=ADVANCED_FACE ( 'NONE', ( #128199 ), #7804, .F. ) ;
#37504=ADVANCED_FACE ( 'NONE', ( #64354 ), #127460, .F. ) ;
#37506=VERTEX_POINT ( 'NONE', #84001 ) ;
#37507=LINE ( 'NONE', #12153, #48521 ) ;
#37508=FACE_OUTER_BOUND ( 'NONE', #1614, .T. ) ;
#37509=LINE ( 'NONE', #59281, #82251 ) ;
#37510=ORIENTED_EDGE ( 'NONE', *, *, #26144, .F. ) ;
#37511=CARTESIAN_POINT ( 'NONE',  ( 7.785015802758053383, -3.740707523384244837, 15.76143240460126194 ) ) ;
#37513=AXIS2_PLACEMENT_3D ( 'NONE', #89018, #33914, #46236 ) ;
#37514=CARTESIAN_POINT ( 'NONE',  ( 4.001930566820951718, -22.22500000000000142, 4.500000000000000888 ) ) ;
#37516=VERTEX_POINT ( 'NONE', #139068 ) ;
#37517=VERTEX_POINT ( 'NONE', #73113 ) ;
#37518=ORIENTED_EDGE ( 'NONE', *, *, #17918, .F. ) ;
#37520=VERTEX_POINT ( 'NONE', #62227 ) ;
#37522=DIRECTION ( 'NONE',  ( -0.7071067811865487940, 0.7071067811865463515, 0.000000000000000000 ) ) ;
#37523=DIRECTION ( 'NONE',  ( -0.7071067811865487940, 0.7071067811865463515, 0.000000000000000000 ) ) ;
#37524=CARTESIAN_POINT ( 'NONE',  ( -20.99451991528748707, 28.92564299267952777, 4.000000000000000000 ) ) ;
#37525=ORIENTED_EDGE ( 'NONE', *, *, #24609, .T. ) ;
#37528=CARTESIAN_POINT ( 'NONE',  ( -57.18398860626899705, 28.73617430169827358, 5.000000000000000000 ) ) ;
#37529=VECTOR ( 'NONE', #41859, 1000.000000000000000 ) ;
#37530=AXIS2_PLACEMENT_3D ( 'NONE', #121844, #1488, #2939 ) ;
#37532=ORIENTED_EDGE ( 'NONE', *, *, #81670, .F. ) ;
#37533=CARTESIAN_POINT ( 'NONE',  ( 35.99451991528749772, 28.92564299267963079, 4.000000000000000000 ) ) ;
#37534=VECTOR ( 'NONE', #28584, 1000.000000000000114 ) ;
#37535=CARTESIAN_POINT ( 'NONE',  ( -63.18398860626900415, 28.73617430169831621, 5.000000000000000000 ) ) ;
#37536=EDGE_LOOP ( 'NONE', ( #31424, #42120, #105609, #96693 ) ) ;
#37537=VERTEX_POINT ( 'NONE', #85372 ) ;
#37538=EDGE_CURVE ( 'NONE', #40356, #122205, #22243, .T. ) ;
#37539=CARTESIAN_POINT ( 'NONE',  ( 57.48921356237308800, -27.52281430457095368, 5.000000000000000000 ) ) ;
#37540=DIRECTION ( 'NONE',  ( -0.7071067811865487940, 0.7071067811865463515, 0.000000000000000000 ) ) ;
#37541=CARTESIAN_POINT ( 'NONE',  ( 24.18398860626899705, 28.73617430169804265, 5.000000000000000000 ) ) ;
#37543=DIRECTION ( 'NONE',  ( -0.7071067811865487940, 0.7071067811865463515, -0.000000000000000000 ) ) ;
#37544=FACE_OUTER_BOUND ( 'NONE', #23625, .T. ) ;
#37545=DIRECTION ( 'NONE',  ( -0.7071067811865486830, -0.7071067811865464625, -0.000000000000000000 ) ) ;
#37546=ORIENTED_EDGE ( 'NONE', *, *, #56028, .T. ) ;
#37547=ORIENTED_EDGE ( 'NONE', *, *, #43251, .F. ) ;
#37548=CARTESIAN_POINT ( 'NONE',  ( -26.99999999999980815, 16.93112307739200872, 4.000000000000000000 ) ) ;
#37549=VERTEX_POINT ( 'NONE', #141941 ) ;
#37550=EDGE_CURVE ( 'NONE', #45664, #93680, #44791, .T. ) ;
#37551=VECTOR ( 'NONE', #101367, 1000.000000000000000 ) ;
#37554=ADVANCED_FACE ( 'NONE', ( #32445 ), #22946, .T. ) ;
#37555=EDGE_LOOP ( 'NONE', ( #119156, #126368, #92669, #57712 ) ) ;
#37556=DIRECTION ( 'NONE',  ( -0.7071067811865486830, 0.7071067811865464625, 0.000000000000000000 ) ) ;
#37557=CARTESIAN_POINT ( 'NONE',  ( -0.4751261278504552710, 14.25929247661557397, 9.797011795316636906 ) ) ;
#37558=VECTOR ( 'NONE', #47950, 1000.000000000000000 ) ;
#37559=CARTESIAN_POINT ( 'NONE',  ( -13.10966639810773771, 3.759292476615678336, 4.164048746910666843 ) ) ;
#37560=AXIS2_PLACEMENT_3D ( 'NONE', #17502, #105920, #62460 ) ;
#37561=DIRECTION ( 'NONE',  ( 0.7071067811865486830, -0.7071067811865464625, -0.000000000000000000 ) ) ;
#37562=VERTEX_POINT ( 'NONE', #54229 ) ;
#37563=PLANE ( 'NONE',  #37858 ) ;
#37564=LINE ( 'NONE', #115774, #122988 ) ;
#37566=CARTESIAN_POINT ( 'NONE',  ( 2.816011393730999401, 28.73617430169785436, 5.000000000000000000 ) ) ;
#37567=ORIENTED_EDGE ( 'NONE', *, *, #76291, .F. ) ;
#37568=ADVANCED_FACE ( 'NONE', ( #12805 ), #65089, .F. ) ;
#37569=VERTEX_POINT ( 'NONE', #497 ) ;
#37570=CARTESIAN_POINT ( 'NONE',  ( 26.84387692260740366, -22.22500000000000142, 4.000000000000000000 ) ) ;
#37571=EDGE_LOOP ( 'NONE', ( #97036, #67605, #110273, #132794 ) ) ;
#37572=ORIENTED_EDGE ( 'NONE', *, *, #48352, .F. ) ;
#37574=VECTOR ( 'NONE', #68270, 1000.000000000000000 ) ;
#37575=ORIENTED_EDGE ( 'NONE', *, *, #37267, .F. ) ;
#37576=CARTESIAN_POINT ( 'NONE',  ( 34.92499999999998295, 14.81665438641030264, 4.500000000000000888 ) ) ;
#37577=CARTESIAN_POINT ( 'NONE',  ( -10.49999999999992006, 18.43112307739199451, 4.000000000000000000 ) ) ;
#37579=FACE_OUTER_BOUND ( 'NONE', #16001, .T. ) ;
#37580=DIRECTION ( 'NONE',  ( 0.3543493200069162685, -0.000000000000000000, -0.9351131265310288487 ) ) ;
#37581=VECTOR ( 'NONE', #18572, 1000.000000000000000 ) ;
#37582=CARTESIAN_POINT ( 'NONE',  ( 51.18398860626899705, 28.73617430169823095, 5.000000000000000000 ) ) ;
#37583=PLANE ( 'NONE',  #76830 ) ;
#37584=PLANE ( 'NONE',  #125063 ) ;
#37586=FACE_OUTER_BOUND ( 'NONE', #17592, .T. ) ;
#37587=CARTESIAN_POINT ( 'NONE',  ( -28.82816939922332722, 9.759292476615623713, 4.000000000000000000 ) ) ;
#37588=EDGE_LOOP ( 'NONE', ( #86653, #57128, #25582, #37986 ) ) ;
#37589=DIRECTION ( 'NONE',  ( -0.6830127018922180770, -0.6830127018922204085, -0.2588190451025213501 ) ) ;
#37590=DIRECTION ( 'NONE',  ( 0.7071067811865486830, -0.7071067811865464625, -0.000000000000000000 ) ) ;
#37591=ORIENTED_EDGE ( 'NONE', *, *, #129911, .T. ) ;
#37592=ORIENTED_EDGE ( 'NONE', *, *, #97667, .T. ) ;
#37593=VECTOR ( 'NONE', #55820, 1000.000000000000000 ) ;
#37594=DIRECTION ( 'NONE',  ( 0.7071067811865486830, -0.7071067811865464625, -0.000000000000000000 ) ) ;
#37595=ORIENTED_EDGE ( 'NONE', *, *, #10993, .T. ) ;
#37596=CARTESIAN_POINT ( 'NONE',  ( 0.000000000000000000, 0.000000000000000000, 5.000000000000000000 ) ) ;
#37597=FACE_OUTER_BOUND ( 'NONE', #105445, .T. ) ;
#37598=CARTESIAN_POINT ( 'NONE',  ( 14.99451991528749595, 28.92564299267948513, 4.000000000000000000 ) ) ;
#37600=EDGE_CURVE ( 'NONE', #73568, #24833, #88980, .T. ) ;
#37603=EDGE_LOOP ( 'NONE', ( #119210, #64964, #56605, #17711 ) ) ;
#37604=EDGE_CURVE ( 'NONE', #34897, #72728, #33879, .T. ) ;
#37606=EDGE_CURVE ( 'NONE', #332, #74632, #43323, .T. ) ;
#37607=FACE_OUTER_BOUND ( 'NONE', #6278, .T. ) ;
#37609=ORIENTED_EDGE ( 'NONE', *, *, #72832, .T. ) ;
#37610=ORIENTED_EDGE ( 'NONE', *, *, #128815, .F. ) ;
#37611=EDGE_CURVE ( 'NONE', #126734, #85586, #109280, .T. ) ;
#37612=ORIENTED_EDGE ( 'NONE', *, *, #109442, .T. ) ;
#37614=CARTESIAN_POINT ( 'NONE',  ( -42.18398860626899705, 28.73617430169816700, 5.000000000000000000 ) ) ;
#37615=VECTOR ( 'NONE', #116606, 1000.000000000000000 ) ;
#37617=DIRECTION ( 'NONE',  ( -0.7071067811865486830, -0.7071067811865464625, 0.000000000000000000 ) ) ;
#37618=VECTOR ( 'NONE', #118061, 1000.000000000000227 ) ;
#37619=EDGE_CURVE ( 'NONE', #59256, #23231, #33193, .T. ) ;
#37621=ORIENTED_EDGE ( 'NONE', *, *, #132424, .T. ) ;
#37622=DIRECTION ( 'NONE',  ( -0.3543493200069162685, -0.000000000000000000, -0.9351131265310288487 ) ) ;
#37623=VECTOR ( 'NONE', #115463, 1000.000000000000000 ) ;
#37624=CARTESIAN_POINT ( 'NONE',  ( 8.510786437626906675, -27.52281430457049183, 5.000000000000000000 ) ) ;
#37626=DIRECTION ( 'NONE',  ( -0.3543493200069162685, -0.000000000000000000, -0.9351131265310288487 ) ) ;
#37627=ADVANCED_FACE ( 'NONE', ( #1207 ), #9957, .F. ) ;
#37628=CARTESIAN_POINT ( 'NONE',  ( 5.915086768062343126, -12.74070752338415602, 18.74364270924355935 ) ) ;
#37629=DIRECTION ( 'NONE',  ( -0.6830127018922181881, 0.6830127018922202975, -0.2588190451025214056 ) ) ;
#37631=CARTESIAN_POINT ( 'NONE',  ( -3.328169399223503966, 2.259292476615697876, 4.000000000000000000 ) ) ;
#37632=VECTOR ( 'NONE', #95792, 1000.000000000000000 ) ;
#37633=VECTOR ( 'NONE', #130743, 1000.000000000000000 ) ;
#37634=DIRECTION ( 'NONE',  ( -0.7071067811865486830, -0.7071067811865464625, 0.000000000000000000 ) ) ;
#37635=EDGE_LOOP ( 'NONE', ( #30500, #101276, #126699, #88419 ) ) ;
#37636=ADVANCED_FACE ( 'NONE', ( #121571 ), #131762, .F. ) ;
#37637=DIRECTION ( 'NONE',  ( 0.7071067811865486830, -0.7071067811865464625, -0.000000000000000000 ) ) ;
#37639=VERTEX_POINT ( 'NONE', #44036 ) ;
#37640=EDGE_LOOP ( 'NONE', ( #7952, #39862, #122994, #118432 ) ) ;
#37641=EDGE_CURVE ( 'NONE', #31122, #55910, #89666, .T. ) ;
#37642=CARTESIAN_POINT ( 'NONE',  ( 0.7071067811865432429, 20.25929247661551003, 5.000000000000000000 ) ) ;
#37643=DIRECTION ( 'NONE',  ( -0.7071067811865487940, 0.7071067811865463515, -0.000000000000000000 ) ) ;
#37644=DIRECTION ( 'NONE',  ( -0.6830127018922181881, 0.6830127018922202975, -0.2588190451025214056 ) ) ;
#37645=VERTEX_POINT ( 'NONE', #54920 ) ;
#37648=EDGE_LOOP ( 'NONE', ( #74619, #32151, #65709, #109035 ) ) ;
#37649=EDGE_CURVE ( 'NONE', #87036, #61991, #133895, .T. ) ;
#37650=DIRECTION ( 'NONE',  ( 0.7071067811865487940, -0.7071067811865463515, 0.000000000000000000 ) ) ;
#37653=DIRECTION ( 'NONE',  ( 0.6830127018922181881, 0.6830127018922202975, -0.2588190451025214056 ) ) ;
#37654=VECTOR ( 'NONE', #78634, 1000.000000000000000 ) ;
#37655=DIRECTION ( 'NONE',  ( 0.7071067811865487940, -0.7071067811865463515, 0.000000000000000000 ) ) ;
#37656=DIRECTION ( 'NONE',  ( 0.6830127018922180770, -0.6830127018922204085, -0.2588190451025213501 ) ) ;
#37657=CARTESIAN_POINT ( 'NONE',  ( -12.48921356237309155, -27.52281430457064104, 5.000000000000000000 ) ) ;
#37662=LINE ( 'NONE', #92012, #263 ) ;
#37663=FACE_OUTER_BOUND ( 'NONE', #116574, .T. ) ;
#37666=ORIENTED_EDGE ( 'NONE', *, *, #53875, .F. ) ;
#37668=ORIENTED_EDGE ( 'NONE', *, *, #50311, .T. ) ;
#37669=EDGE_LOOP ( 'NONE', ( #32133, #86394, #47511, #8441 ) ) ;
#37671=VECTOR ( 'NONE', #17927, 1000.000000000000227 ) ;
#37673=DIRECTION ( 'NONE',  ( -0.7071067811865487940, 0.7071067811865463515, 0.000000000000000000 ) ) ;
#37675=AXIS2_PLACEMENT_3D ( 'NONE', #62118, #62840, #93999 ) ;
#37677=ORIENTED_EDGE ( 'NONE', *, *, #109516, .T. ) ;
#37678=CARTESIAN_POINT ( 'NONE',  ( 13.49999999999991296, -4.533600742197688938, 5.000000000000000000 ) ) ;
#37679=DIRECTION ( 'NONE',  ( 1.000000000000000000, 0.000000000000000000, 0.000000000000000000 ) ) ;
#37682=PLANE ( 'NONE',  #35437 ) ;
#37684=DIRECTION ( 'NONE',  ( 0.7071067811865486830, -0.7071067811865464625, -0.000000000000000000 ) ) ;
#37685=LINE ( 'NONE', #73169, #80019 ) ;
#37686=LINE ( 'NONE', #46447, #65458 ) ;
#37688=CARTESIAN_POINT ( 'NONE',  ( -32.20710678118632586, -5.240707523384223521, 5.000000000000000000 ) ) ;
#37689=EDGE_CURVE ( 'NONE', #72412, #126512, #123022, .T. ) ;
#37690=CARTESIAN_POINT ( 'NONE',  ( -33.18398860626899705, 28.73617430169810305, 5.000000000000000000 ) ) ;
#37691=EDGE_LOOP ( 'NONE', ( #121077, #53756, #39227, #83202 ) ) ;
#37692=VERTEX_POINT ( 'NONE', #120118 ) ;
#37694=ORIENTED_EDGE ( 'NONE', *, *, #115130, .T. ) ;
#37695=ADVANCED_FACE ( 'NONE', ( #76684 ), #20827, .F. ) ;
#37696=VECTOR ( 'NONE', #46673, 1000.000000000000000 ) ;
#37697=CARTESIAN_POINT ( 'NONE',  ( 30.29974487139158867, -27.71228299555227537, 4.000000000000000000 ) ) ;
#37698=AXIS2_PLACEMENT_3D ( 'NONE', #62815, #19978, #52616 ) ;
#37699=LINE ( 'NONE', #124685, #78125 ) ;
#37701=CARTESIAN_POINT ( 'NONE',  ( 3.489213562373097322, -27.52281430457057709, 5.000000000000000000 ) ) ;
#37702=CARTESIAN_POINT ( 'NONE',  ( -51.18398860626899705, 28.73617430169823095, 5.000000000000000000 ) ) ;
#37704=ORIENTED_EDGE ( 'NONE', *, *, #79198, .F. ) ;
#37705=EDGE_CURVE ( 'NONE', #43034, #50767, #14249, .T. ) ;
#37706=ORIENTED_EDGE ( 'NONE', *, *, #98814, .F. ) ;
#37707=PLANE ( 'NONE',  #6009 ) ;
#37708=VECTOR ( 'NONE', #79656, 1000.000000000000000 ) ;
#37709=CARTESIAN_POINT ( 'NONE',  ( -30.18398860626900060, 28.73617430169808173, 5.000000000000000000 ) ) ;
#37710=CARTESIAN_POINT ( 'NONE',  ( -24.69524342170288023, 1.235879655689124501, 4.000000000000000000 ) ) ;
#37711=ORIENTED_EDGE ( 'NONE', *, *, #71330, .F. ) ;
#37712=EDGE_LOOP ( 'NONE', ( #99813, #135063, #55865, #55304 ) ) ;
#37713=ADVANCED_FACE ( 'NONE', ( #70804 ), #135345, .T. ) ;
#37714=ORIENTED_EDGE ( 'NONE', *, *, #50250, .F. ) ;
#37715=CARTESIAN_POINT ( 'NONE',  ( 23.99999999999983302, -15.03360074219758147, 5.000000000000000000 ) ) ;
#37718=DIRECTION ( 'NONE',  ( -0.7071067811865486830, -0.7071067811865464625, 0.000000000000000000 ) ) ;
#37719=ORIENTED_EDGE ( 'NONE', *, *, #39306, .T. ) ;
#37720=ORIENTED_EDGE ( 'NONE', *, *, #56425, .F. ) ;
#37721=LINE ( 'NONE', #126150, #91864 ) ;
#37722=ORIENTED_EDGE ( 'NONE', *, *, #119815, .T. ) ;
#37723=ORIENTED_EDGE ( 'NONE', *, *, #75797, .T. ) ;
#37725=CARTESIAN_POINT ( 'NONE',  ( -14.59122188827396549, 7.143407583703162089, 5.000000000000000000 ) ) ;
#37727=CARTESIAN_POINT ( 'NONE',  ( 63.29974487139158867, -27.71228299555250274, 4.000000000000000000 ) ) ;
#37728=EDGE_CURVE ( 'NONE', #131836, #104249, #38166, .T. ) ;
#37730=CARTESIAN_POINT ( 'NONE',  ( 32.99999999999977263, 1.552185695429149304, 5.000000000000000000 ) ) ;
#37731=VECTOR ( 'NONE', #10448, 999.9999999999998863 ) ;
#37732=CARTESIAN_POINT ( 'NONE',  ( -23.24139925780185223, 21.72500000000000853, 5.000000000000000000 ) ) ;
#37733=VECTOR ( 'NONE', #92188, 1000.000000000000000 ) ;
#37735=FACE_OUTER_BOUND ( 'NONE', #88678, .T. ) ;
#37736=PLANE ( 'NONE',  #109146 ) ;
#37737=LINE ( 'NONE', #60202, #53681 ) ;
#37738=FACE_BOUND ( 'NONE', #118095, .T. ) ;
#37739=ORIENTED_EDGE ( 'NONE', *, *, #101737, .F. ) ;
#37740=CARTESIAN_POINT ( 'NONE',  ( 12.79289321881335617, 18.75929247661552068, 5.000000000000000000 ) ) ;
#37742=EDGE_CURVE ( 'NONE', #56522, #132816, #137473, .T. ) ;
#37743=ORIENTED_EDGE ( 'NONE', *, *, #44984, .F. ) ;
#37744=DIRECTION ( 'NONE',  ( 0.7071067811865487940, 0.7071067811865463515, 0.000000000000000000 ) ) ;
#37745=ORIENTED_EDGE ( 'NONE', *, *, #106630, .F. ) ;
#37747=VERTEX_POINT ( 'NONE', #80953 ) ;
#37748=ORIENTED_EDGE ( 'NONE', *, *, #55217, .F. ) ;
#37751=ORIENTED_EDGE ( 'NONE', *, *, #54012, .T. ) ;
#37752=VECTOR ( 'NONE', #83657, 1000.000000000000000 ) ;
#37753=CARTESIAN_POINT ( 'NONE',  ( 4.785015802758072034, -3.740707523384244837, 15.76143240460125128 ) ) ;
#37754=CARTESIAN_POINT ( 'NONE',  ( -24.32816939922335564, 20.25929247661551003, 4.000000000000000000 ) ) ;
#37755=CARTESIAN_POINT ( 'NONE',  ( -0.08491323193762084776, -12.74070752338415602, 18.74364270924354514 ) ) ;
#37756=ORIENTED_EDGE ( 'NONE', *, *, #118643, .F. ) ;
#37758=DIRECTION ( 'NONE',  ( 0.7071067811865487940, 0.7071067811865463515, 0.000000000000000000 ) ) ;
#37759=ADVANCED_FACE ( 'NONE', ( #25838 ), #13508, .F. ) ;
#37760=VECTOR ( 'NONE', #87501, 1000.000000000000000 ) ;
#37763=CARTESIAN_POINT ( 'NONE',  ( -39.48921356237310221, -27.52281430457082934, 5.000000000000000000 ) ) ;
#37764=CARTESIAN_POINT ( 'NONE',  ( 51.48921356237309510, -27.52281430457091460, 5.000000000000000000 ) ) ;
#37766=CARTESIAN_POINT ( 'NONE',  ( 57.48921356237308800, -27.52281430457095368, 5.000000000000000000 ) ) ;
#37767=EDGE_LOOP ( 'NONE', ( #85472, #2988, #131860, #104928 ) ) ;
#37768=VERTEX_POINT ( 'NONE', #35325 ) ;
#37769=ORIENTED_EDGE ( 'NONE', *, *, #40373, .F. ) ;
#37770=ORIENTED_EDGE ( 'NONE', *, *, #37600, .T. ) ;
#37771=ORIENTED_EDGE ( 'NONE', *, *, #57061, .T. ) ;
#37772=ORIENTED_EDGE ( 'NONE', *, *, #17897, .F. ) ;
#37773=LINE ( 'NONE', #26868, #137100 ) ;
#37774=LINE ( 'NONE', #92117, #23092 ) ;
#37775=EDGE_LOOP ( 'NONE', ( #65114, #91699, #124224, #72924 ) ) ;
#37776=PLANE ( 'NONE',  #94993 ) ;
#37777=ORIENTED_EDGE ( 'NONE', *, *, #64465, .T. ) ;
#37778=CARTESIAN_POINT ( 'NONE',  ( 26.01088028653929740, -22.02621442084248216, 4.990779571109220214 ) ) ;
#37779=VECTOR ( 'NONE', #36895, 1000.000000000000000 ) ;
#37780=CARTESIAN_POINT ( 'NONE',  ( 29.99451991528749417, 28.92564299267958816, 4.000000000000000000 ) ) ;
#37781=EDGE_CURVE ( 'NONE', #57095, #69883, #42615, .T. ) ;
#37782=VECTOR ( 'NONE', #100380, 999.9999999999998863 ) ;
#37784=VERTEX_POINT ( 'NONE', #92505 ) ;
#37786=DIRECTION ( 'NONE',  ( -0.6830127018922180770, -0.6830127018922204085, -0.2588190451025213501 ) ) ;
#37787=ADVANCED_FACE ( 'NONE', ( #59918 ), #90381, .F. ) ;
#37789=DIRECTION ( 'NONE',  ( 0.7071067811865486830, -0.7071067811865464625, -0.000000000000000000 ) ) ;
#37790=EDGE_LOOP ( 'NONE', ( #128683, #63531, #128097, #58135 ) ) ;
#37793=EDGE_CURVE ( 'NONE', #94260, #124605, #69369, .T. ) ;
#37794=CARTESIAN_POINT ( 'NONE',  ( 0.000000000000000000, 12.83542986846997813, -1.025386466790367379 ) ) ;
#37795=VERTEX_POINT ( 'NONE', #113546 ) ;
#37796=VECTOR ( 'NONE', #129284, 1000.000000000000227 ) ;
#37797=DIRECTION ( 'NONE',  ( 0.7071067811865486830, -0.7071067811865464625, -0.000000000000000000 ) ) ;
#37798=CARTESIAN_POINT ( 'NONE',  ( 8.510786437626906675, -27.52281430457049183, 5.000000000000000000 ) ) ;
#37799=DIRECTION ( 'NONE',  ( -0.7071067811865487940, 0.7071067811865463515, 0.000000000000000000 ) ) ;
#37801=ADVANCED_FACE ( 'NONE', ( #3350 ), #47641, .F. ) ;
#37803=EDGE_LOOP ( 'NONE', ( #125217, #13372, #62101, #105116, #68128 ) ) ;
#37804=CARTESIAN_POINT ( 'NONE',  ( -24.96654721599509941, 3.964575861396866685, 4.000000000000000000 ) ) ;
#37805=CARTESIAN_POINT ( 'NONE',  ( 19.99806943317887686, -22.22500000000000142, 4.500000000000000888 ) ) ;
#37806=CARTESIAN_POINT ( 'NONE',  ( 0.000000000000000000, 0.000000000000000000, 5.000000000000000000 ) ) ;
#37807=VERTEX_POINT ( 'NONE', #126563 ) ;
#37808=LINE ( 'NONE', #26905, #139226 ) ;
#37809=VECTOR ( 'NONE', #112132, 1000.000000000000000 ) ;
#37810=DIRECTION ( 'NONE',  ( -0.7071067811865487940, 0.7071067811865463515, 0.000000000000000000 ) ) ;
#37811=ORIENTED_EDGE ( 'NONE', *, *, #134014, .F. ) ;
#37812=EDGE_CURVE ( 'NONE', #22385, #123961, #82386, .T. ) ;
#37813=CARTESIAN_POINT ( 'NONE',  ( -32.99999999999976552, 1.552185695429151080, 5.000000000000000000 ) ) ;
#37815=EDGE_CURVE ( 'NONE', #81604, #91460, #59230, .T. ) ;
#37816=VERTEX_POINT ( 'NONE', #49043 ) ;
#37817=VECTOR ( 'NONE', #101860, 1000.000000000000000 ) ;
#37818=DIRECTION ( 'NONE',  ( -0.7071067811865487940, 0.7071067811865463515, 0.000000000000000000 ) ) ;
#37819=FACE_OUTER_BOUND ( 'NONE', #65674, .T. ) ;
#37820=ORIENTED_EDGE ( 'NONE', *, *, #36686, .F. ) ;
#37821=CARTESIAN_POINT ( 'NONE',  ( -63.48921356237309510, -27.52281430457099631, 5.000000000000000000 ) ) ;
#37822=EDGE_CURVE ( 'NONE', #78479, #74127, #101256, .T. ) ;
#37823=CARTESIAN_POINT ( 'NONE',  ( 8.999999999999937828, 12.25461709320621928, -10.07315571508695129 ) ) ;
#37825=DIRECTION ( 'NONE',  ( 0.3543493200069162685, -0.000000000000000000, -0.9351131265310288487 ) ) ;
#37826=LINE ( 'NONE', #61037, #106768 ) ;
#37827=DIRECTION ( 'NONE',  ( 0.7071067811865487940, 0.7071067811865463515, 0.000000000000000000 ) ) ;
#37828=DIRECTION ( 'NONE',  ( 0.3543493200069162685, -0.000000000000000000, -0.9351131265310288487 ) ) ;
#37830=AXIS2_PLACEMENT_3D ( 'NONE', #140481, #82549, #72432 ) ;
#37831=PLANE ( 'NONE',  #56359 ) ;
#37832=CARTESIAN_POINT ( 'NONE',  ( 54.29974487139159578, -27.71228299555243879, 4.000000000000000000 ) ) ;
#37833=DIRECTION ( 'NONE',  ( 0.7071067811865487940, 0.7071067811865463515, 0.000000000000000000 ) ) ;
#37834=CARTESIAN_POINT ( 'NONE',  ( -16.82816939922341604, -5.240707523384227073, 4.000000000000000000 ) ) ;
#37835=ORIENTED_EDGE ( 'NONE', *, *, #126033, .T. ) ;
#37836=VECTOR ( 'NONE', #9350, 1000.000000000000000 ) ;
#37838=ORIENTED_EDGE ( 'NONE', *, *, #30578, .T. ) ;
#37840=ORIENTED_EDGE ( 'NONE', *, *, #138788, .F. ) ;
#37842=VERTEX_POINT ( 'NONE', #72964 ) ;
#37847=LINE ( 'NONE', #117491, #99502 ) ;
#37848=ORIENTED_EDGE ( 'NONE', *, *, #73374, .T. ) ;
#37850=DIRECTION ( 'NONE',  ( 1.000000000000000000, 0.000000000000000000, 0.000000000000000000 ) ) ;
#37853=VERTEX_POINT ( 'NONE', #106227 ) ;
#37855=LINE ( 'NONE', #113961, #49232 ) ;
#37856=DIRECTION ( 'NONE',  ( 1.000000000000000000, 0.000000000000000000, 0.000000000000000000 ) ) ;
#37858=AXIS2_PLACEMENT_3D ( 'NONE', #48419, #81800, #139012 ) ;
#37859=CARTESIAN_POINT ( 'NONE',  ( -21.71715331601274102, -2.164967620583693630, 5.000000000000000000 ) ) ;
#37860=DIRECTION ( 'NONE',  ( 0.7071067811865487940, -0.7071067811865463515, 0.000000000000000000 ) ) ;
#37862=EDGE_CURVE ( 'NONE', #18615, #30768, #95375, .T. ) ;
#37863=DIRECTION ( 'NONE',  ( -0.000000000000000000, 0.3543493200069153248, 0.9351131265310292928 ) ) ;
#37865=DIRECTION ( 'NONE',  ( -0.7071067811865486830, -0.7071067811865464625, 0.000000000000000000 ) ) ;
#37866=ORIENTED_EDGE ( 'NONE', *, *, #110283, .F. ) ;
#37867=ORIENTED_EDGE ( 'NONE', *, *, #81097, .F. ) ;
#37870=ORIENTED_EDGE ( 'NONE', *, *, #60751, .T. ) ;
#37871=LINE ( 'NONE', #126976, #127057 ) ;
#37872=LINE ( 'NONE', #95789, #98729 ) ;
#37873=ORIENTED_EDGE ( 'NONE', *, *, #27572, .T. ) ;
#37874=CARTESIAN_POINT ( 'NONE',  ( 48.29974487139158867, -27.71228299555239971, 4.000000000000000000 ) ) ;
#37875=VECTOR ( 'NONE', #109058, 1000.000000000000000 ) ;
#37876=DIRECTION ( 'NONE',  ( -0.7071067811865486830, -0.7071067811865464625, 0.000000000000000000 ) ) ;
#37877=CARTESIAN_POINT ( 'NONE',  ( -11.29289321881337749, 14.25929247661557042, 5.000000000000000000 ) ) ;
#37879=AXIS2_PLACEMENT_3D ( 'NONE', #30081, #118521, #19219 ) ;
#37880=ORIENTED_EDGE ( 'NONE', *, *, #34925, .F. ) ;
#37881=EDGE_CURVE ( 'NONE', #143315, #15762, #127718, .T. ) ;
#37882=DIRECTION ( 'NONE',  ( -0.6830127018922181881, 0.6830127018922202975, -0.2588190451025214056 ) ) ;
#37883=ORIENTED_EDGE ( 'NONE', *, *, #52232, .F. ) ;
#37885=LINE ( 'NONE', #28423, #5946 ) ;
#37887=VECTOR ( 'NONE', #108335, 999.9999999999998863 ) ;
#37888=DIRECTION ( 'NONE',  ( 0.7071067811865487940, 0.7071067811865463515, -0.000000000000000000 ) ) ;
#37889=ORIENTED_EDGE ( 'NONE', *, *, #67875, .T. ) ;
#37890=ADVANCED_FACE ( 'NONE', ( #8335 ), #84531, .F. ) ;
#37891=ORIENTED_EDGE ( 'NONE', *, *, #31961, .F. ) ;
#37892=CARTESIAN_POINT ( 'NONE',  ( -18.48921356237309510, -27.52281430457068367, 5.000000000000000000 ) ) ;
#37893=PLANE ( 'NONE',  #134220 ) ;
#37894=CARTESIAN_POINT ( 'NONE',  ( -16.77325839282156750, -11.24070752338416135, 18.24660765846978450 ) ) ;
#37895=LINE ( 'NONE', #35771, #97186 ) ;
#37896=VECTOR ( 'NONE', #117744, 1000.000000000000227 ) ;
#37897=VECTOR ( 'NONE', #37594, 1000.000000000000000 ) ;
#37899=ORIENTED_EDGE ( 'NONE', *, *, #18884, .T. ) ;
#37900=LINE ( 'NONE', #80683, #83579 ) ;
#37901=FACE_OUTER_BOUND ( 'NONE', #58430, .T. ) ;
#37902=ORIENTED_EDGE ( 'NONE', *, *, #110551, .T. ) ;
#37905=DIRECTION ( 'NONE',  ( -0.000000000000000000, 0.000000000000000000, 1.000000000000000000 ) ) ;
#37907=DIRECTION ( 'NONE',  ( -0.7071067811865487940, 0.7071067811865463515, 0.000000000000000000 ) ) ;
#37908=ADVANCED_FACE ( 'NONE', ( #44622 ), #78637, .F. ) ;
#37909=ORIENTED_EDGE ( 'NONE', *, *, #132577, .F. ) ;
#37910=LINE ( 'NONE', #69106, #90920 ) ;
#37911=VECTOR ( 'NONE', #21372, 1000.000000000000000 ) ;
#37912=CARTESIAN_POINT ( 'NONE',  ( 44.99451991528749772, 28.92564299267969474, 4.000000000000000000 ) ) ;
#37913=EDGE_CURVE ( 'NONE', #5176, #132203, #31565, .T. ) ;
#37914=FACE_BOUND ( 'NONE', #55670, .T. ) ;
#37915=CARTESIAN_POINT ( 'NONE',  ( 4.499999999999962697, -12.08601207473289385, -10.46905243149095632 ) ) ;
#37916=CARTESIAN_POINT ( 'NONE',  ( -13.06996025486400725, -0.7407075233842735917, 13.87443053587614195 ) ) ;
#37917=CARTESIAN_POINT ( 'NONE',  ( -48.48921356237309510, -27.52281430457089328, 5.000000000000000000 ) ) ;
#37918=EDGE_CURVE ( 'NONE', #43696, #126534, #142536, .T. ) ;
#37919=VECTOR ( 'NONE', #110057, 1000.000000000000000 ) ;
#37920=CARTESIAN_POINT ( 'NONE',  ( -13.26601651615776767, 1.700382741644379081, 5.000000000000000000 ) ) ;
#37921=LINE ( 'NONE', #50926, #45933 ) ;
#37923=LINE ( 'NONE', #46697, #47207 ) ;
#37924=ORIENTED_EDGE ( 'NONE', *, *, #63155, .T. ) ;
#37925=ORIENTED_EDGE ( 'NONE', *, *, #4790, .T. ) ;
#37927=VECTOR ( 'NONE', #21526, 1000.000000000000000 ) ;
#37929=EDGE_CURVE ( 'NONE', #27002, #64405, #1038, .T. ) ;
#37930=DIRECTION ( 'NONE',  ( 0.7071067811865487940, -0.7071067811865463515, 0.000000000000000000 ) ) ;
#37931=DIRECTION ( 'NONE',  ( -0.7071067811865486830, -0.7071067811865464625, -0.000000000000000000 ) ) ;
#37933=DIRECTION ( 'NONE',  ( 0.7071067811865487940, 0.7071067811865463515, 0.000000000000000000 ) ) ;
#37934=ADVANCED_FACE ( 'NONE', ( #75789 ), #20662, .F. ) ;
#37935=VECTOR ( 'NONE', #99227, 999.9999999999998863 ) ;
#37936=CARTESIAN_POINT ( 'NONE',  ( -2.292893218813446321, 17.25929247661554200, 5.000000000000000000 ) ) ;
#37938=DIRECTION ( 'NONE',  ( -0.7071067811865487940, 0.7071067811865463515, 0.000000000000000000 ) ) ;
#37939=CARTESIAN_POINT ( 'NONE',  ( 2.700255128608413990, -27.71228299555204089, 4.000000000000000000 ) ) ;
#37940=ORIENTED_EDGE ( 'NONE', *, *, #141542, .F. ) ;
#37941=ORIENTED_EDGE ( 'NONE', *, *, #6447, .T. ) ;
#37942=DIRECTION ( 'NONE',  ( -0.7071067811865487940, 0.7071067811865463515, -0.000000000000000000 ) ) ;
#37943=CARTESIAN_POINT ( 'NONE',  ( -14.93988928955970508, -9.740707523384180888, 10.89222023123384453 ) ) ;
#37944=VERTEX_POINT ( 'NONE', #54755 ) ;
#37945=ORIENTED_EDGE ( 'NONE', *, *, #101202, .F. ) ;
#37946=ORIENTED_EDGE ( 'NONE', *, *, #95198, .T. ) ;
#37947=FACE_OUTER_BOUND ( 'NONE', #45199, .T. ) ;
#37948=CARTESIAN_POINT ( 'NONE',  ( 19.05000000000000071, 3.174999999999997158, 4.000000000000000000 ) ) ;
#37949=ORIENTED_EDGE ( 'NONE', *, *, #112087, .T. ) ;
#37950=CARTESIAN_POINT ( 'NONE',  ( -8.292986735706895374, -21.74070752338406010, 4.999753212805224223 ) ) ;
#37952=VECTOR ( 'NONE', #39248, 1000.000000000000000 ) ;
#37954=EDGE_CURVE ( 'NONE', #55140, #35701, #13767, .T. ) ;
#37955=CARTESIAN_POINT ( 'NONE',  ( 29.99999999999979039, 10.21212019023811912, -2.019456568337869129 ) ) ;
#37956=ORIENTED_EDGE ( 'NONE', *, *, #72555, .F. ) ;
#37957=PLANE ( 'NONE',  #48051 ) ;
#37958=EDGE_CURVE ( 'NONE', #2262, #28263, #109101, .T. ) ;
#37959=FACE_OUTER_BOUND ( 'NONE', #59346, .T. ) ;
#37960=CARTESIAN_POINT ( 'NONE',  ( 0.000000000000000000, 0.000000000000000000, 5.000000000000000000 ) ) ;
#37962=ORIENTED_EDGE ( 'NONE', *, *, #139606, .T. ) ;
#37964=ORIENTED_EDGE ( 'NONE', *, *, #136846, .T. ) ;
#37967=VECTOR ( 'NONE', #26360, 1000.000000000000227 ) ;
#37968=EDGE_CURVE ( 'NONE', #37040, #71393, #54063, .T. ) ;
#37969=EDGE_CURVE ( 'NONE', #66281, #63704, #11184, .T. ) ;
#37972=DIRECTION ( 'NONE',  ( 0.3543493200069163240, -0.000000000000000000, -0.9351131265310288487 ) ) ;
#37973=AXIS2_PLACEMENT_3D ( 'NONE', #58148, #91459, #67584 ) ;
#37974=CARTESIAN_POINT ( 'NONE',  ( -21.69326993309585561, -3.740707523384244837, 12.88036043432872546 ) ) ;
#37976=DIRECTION ( 'NONE',  ( -0.7071067811865486830, -0.7071067811865464625, 0.000000000000000000 ) ) ;
#37977=EDGE_LOOP ( 'NONE', ( #72413, #126871, #1865, #51960 ) ) ;
#37978=DIRECTION ( 'NONE',  ( -0.7071067811865486830, -0.7071067811865464625, 0.000000000000000000 ) ) ;
#37979=DIRECTION ( 'NONE',  ( -0.000000000000000000, -0.3543493200069152693, 0.9351131265310292928 ) ) ;
#37980=LINE ( 'NONE', #135849, #132541 ) ;
#37982=DIRECTION ( 'NONE',  ( -0.7071067811865486830, -0.7071067811865464625, -0.000000000000000000 ) ) ;
#37983=ADVANCED_FACE ( 'NONE', ( #86668 ), #98251, .T. ) ;
#37984=DIRECTION ( 'NONE',  ( -0.7071067811865486830, -0.7071067811865464625, 0.000000000000000000 ) ) ;
#37986=ORIENTED_EDGE ( 'NONE', *, *, #82063, .T. ) ;
#37987=EDGE_CURVE ( 'NONE', #68652, #85225, #120680, .T. ) ;
#37988=ORIENTED_EDGE ( 'NONE', *, *, #102830, .T. ) ;
#37991=VECTOR ( 'NONE', #125288, 999.9999999999998863 ) ;
#37993=CARTESIAN_POINT ( 'NONE',  ( 11.71998032010589519, 0.7592924766157104211, 14.27032725228011678 ) ) ;
#37994=VECTOR ( 'NONE', #102138, 1000.000000000000000 ) ;
#37995=LINE ( 'NONE', #138726, #113258 ) ;
#37996=CARTESIAN_POINT ( 'NONE',  ( 11.06845177300853855, 22.22500000000000142, -12.42863820230598648 ) ) ;
#37997=EDGE_CURVE ( 'NONE', #43835, #12885, #32281, .T. ) ;
#37998=CARTESIAN_POINT ( 'NONE',  ( 4.499999999999968914, -7.420205493532893826, -2.617629953481243277 ) ) ;
#37999=ORIENTED_EDGE ( 'NONE', *, *, #126342, .F. ) ;
#38000=CARTESIAN_POINT ( 'NONE',  ( -15.48921356237309510, -27.52281430457066236, 5.000000000000000000 ) ) ;
#38001=PLANE ( 'NONE',  #65508 ) ;
#38002=AXIS2_PLACEMENT_3D ( 'NONE', #20686, #109126, #143190 ) ;
#38003=EDGE_CURVE ( 'NONE', #44481, #5925, #18416, .T. ) ;
#38004=DIRECTION ( 'NONE',  ( -0.7071067811865486830, 0.7071067811865464625, 0.000000000000000000 ) ) ;
#38006=CARTESIAN_POINT ( 'NONE',  ( 20.99999999999985079, -15.03360074219758324, 5.000000000000000000 ) ) ;
#38007=AXIS2_PLACEMENT_3D ( 'NONE', #58300, #68443, #67729 ) ;
#38009=CARTESIAN_POINT ( 'NONE',  ( -31.49999999999977973, 16.46639925780208813, 5.000000000000000000 ) ) ;
#38010=ORIENTED_EDGE ( 'NONE', *, *, #53533, .F. ) ;
#38012=VECTOR ( 'NONE', #14421, 1000.000000000000000 ) ;
#38013=EDGE_CURVE ( 'NONE', #95865, #78216, #141766, .T. ) ;
#38014=CARTESIAN_POINT ( 'NONE',  ( 45.18398860626900415, 28.73617430169818832, 5.000000000000000000 ) ) ;
#38017=CARTESIAN_POINT ( 'NONE',  ( 9.489213562373095101, -27.52281430457062328, 5.000000000000000000 ) ) ;
#38018=CARTESIAN_POINT ( 'NONE',  ( -45.48921356237309510, -27.52281430457087197, 5.000000000000000000 ) ) ;
#38019=EDGE_LOOP ( 'NONE', ( #110200, #142317, #54438, #52542 ) ) ;
#38020=DIRECTION ( 'NONE',  ( -0.6830127018922180770, -0.6830127018922204085, -0.2588190451025213501 ) ) ;
#38021=DIRECTION ( 'NONE',  ( -0.6830127018922181881, 0.6830127018922202975, -0.2588190451025214056 ) ) ;
#38023=FACE_OUTER_BOUND ( 'NONE', #50107, .T. ) ;
#38024=PLANE ( 'NONE',  #10288 ) ;
#38025=DIRECTION ( 'NONE',  ( -0.6830127018922180770, -0.6830127018922204085, -0.2588190451025213501 ) ) ;
#38027=ADVANCED_FACE ( 'NONE', ( #88087 ), #77240, .F. ) ;
#38029=LINE ( 'NONE', #143031, #85440 ) ;
#38031=EDGE_LOOP ( 'NONE', ( #3139, #67933, #76208, #38537 ) ) ;
#38033=DIRECTION ( 'NONE',  ( 0.3543493200069162685, -0.000000000000000000, -0.9351131265310288487 ) ) ;
#38034=DIRECTION ( 'NONE',  ( 0.7071067811865487940, 0.7071067811865463515, 0.000000000000000000 ) ) ;
#38035=DIRECTION ( 'NONE',  ( -0.000000000000000000, 0.3543493200069153248, 0.9351131265310292928 ) ) ;
#38037=AXIS2_PLACEMENT_3D ( 'NONE', #88195, #11293, #55571 ) ;
#38038=CARTESIAN_POINT ( 'NONE',  ( -6.183988606268994381, 28.73617430169791476, 5.000000000000000000 ) ) ;
#38039=CARTESIAN_POINT ( 'NONE',  ( 24.29974487139158867, -27.71228299555223273, 4.000000000000000000 ) ) ;
#38041=DIRECTION ( 'NONE',  ( -0.6830127018922181881, 0.6830127018922202975, -0.2588190451025214056 ) ) ;
#38042=EDGE_LOOP ( 'NONE', ( #137086, #12869, #20891, #84899 ) ) ;
#38044=DIRECTION ( 'NONE',  ( 0.7071067811865486830, -0.7071067811865464625, -0.000000000000000000 ) ) ;
#38046=FACE_OUTER_BOUND ( 'NONE', #5204, .T. ) ;
#38047=CARTESIAN_POINT ( 'NONE',  ( -6.183988606268994381, 28.73617430169791476, 5.000000000000000000 ) ) ;
#38048=DIRECTION ( 'NONE',  ( 0.7071067811865487940, -0.7071067811865463515, 0.000000000000000000 ) ) ;
#38050=ORIENTED_EDGE ( 'NONE', *, *, #122923, .T. ) ;
#38051=LINE ( 'NONE', #62653, #120096 ) ;
#38053=CARTESIAN_POINT ( 'NONE',  ( -24.41161490594814509, 22.22500000000000497, 4.777194822843814137 ) ) ;
#38054=VECTOR ( 'NONE', #109225, 999.9999999999998863 ) ;
#38055=LINE ( 'NONE', #124328, #120163 ) ;
#38056=ORIENTED_EDGE ( 'NONE', *, *, #140323, .T. ) ;
#38057=AXIS2_PLACEMENT_3D ( 'NONE', #85777, #29961, #20499 ) ;
#38059=CARTESIAN_POINT ( 'NONE',  ( 0.000000000000000000, 18.08204922493373346, 0.9627537363044872398 ) ) ;
#38060=VECTOR ( 'NONE', #57814, 1000.000000000000000 ) ;
#38061=CARTESIAN_POINT ( 'NONE',  ( -54.48921356237310221, -27.52281430457093236, 5.000000000000000000 ) ) ;
#38063=ADVANCED_FACE ( 'NONE', ( #14795 ), #15472, .F. ) ;
#38065=LINE ( 'NONE', #50360, #64036 ) ;
#38066=VERTEX_POINT ( 'NONE', #46027 ) ;
#38067=ORIENTED_EDGE ( 'NONE', *, *, #70748, .F. ) ;
#38068=CARTESIAN_POINT ( 'NONE',  ( -16.49999999999988987, -4.216083040037264418, -7.486842126848618051 ) ) ;
#38069=DIRECTION ( 'NONE',  ( 0.7071067811865487940, 0.7071067811865463515, 0.000000000000000000 ) ) ;
#38070=ORIENTED_EDGE ( 'NONE', *, *, #132246, .T. ) ;
#38072=FACE_OUTER_BOUND ( 'NONE', #16669, .T. ) ;
#38073=EDGE_CURVE ( 'NONE', #117034, #106208, #103915, .T. ) ;
#38074=EDGE_LOOP ( 'NONE', ( #84523, #73916, #63869, #126118, #21778 ) ) ;
#38076=LINE ( 'NONE', #27891, #49414 ) ;
#38079=FACE_BOUND ( 'NONE', #70654, .T. ) ;
#38080=PLANE ( 'NONE',  #3828 ) ;
#38082=ADVANCED_FACE ( 'NONE', ( #59067 ), #37272, .F. ) ;
#38083=CARTESIAN_POINT ( 'NONE',  ( 0.000000000000000000, 0.000000000000000000, 5.000000000000000000 ) ) ;
#38084=CARTESIAN_POINT ( 'NONE',  ( 34.49999999999975131, 8.319652575858413002, -8.582050562765747515 ) ) ;
#38085=VECTOR ( 'NONE', #76103, 1000.000000000000000 ) ;
#38086=EDGE_CURVE ( 'NONE', #139562, #6765, #90955, .T. ) ;
#38089=ORIENTED_EDGE ( 'NONE', *, *, #106045, .F. ) ;
#38090=VECTOR ( 'NONE', #121373, 999.9999999999998863 ) ;
#38091=ORIENTED_EDGE ( 'NONE', *, *, #109523, .F. ) ;
#38094=ADVANCED_FACE ( 'NONE', ( #93076 ), #81515, .F. ) ;
#38095=LINE ( 'NONE', #112082, #2527 ) ;
#38097=EDGE_CURVE ( 'NONE', #1886, #125922, #14068, .T. ) ;
#38098=AXIS2_PLACEMENT_3D ( 'NONE', #61321, #105459, #6124 ) ;
#38099=FACE_OUTER_BOUND ( 'NONE', #124135, .T. ) ;
#38100=EDGE_LOOP ( 'NONE', ( #143099, #68634, #18780, #134089 ) ) ;
#38103=CARTESIAN_POINT ( 'NONE',  ( -6.781626882924903121, 21.74787736706805319, 4.999607392498050196 ) ) ;
#38104=DIRECTION ( 'NONE',  ( -0.7071067811865487940, 0.7071067811865463515, -0.000000000000000000 ) ) ;
#38106=DIRECTION ( 'NONE',  ( 0.6830127018922180770, -0.6830127018922204085, -0.2588190451025213501 ) ) ;
#38109=DIRECTION ( 'NONE',  ( 0.3543493200069162685, -0.000000000000000000, -0.9351131265310288487 ) ) ;
#38110=ORIENTED_EDGE ( 'NONE', *, *, #10991, .F. ) ;
#38111=CARTESIAN_POINT ( 'NONE',  ( 72.18398860626899705, 28.73617430169837661, 5.000000000000000000 ) ) ;
#38112=CARTESIAN_POINT ( 'NONE',  ( 60.29974487139158867, -27.71228299555248142, 4.000000000000000000 ) ) ;
#38113=ORIENTED_EDGE ( 'NONE', *, *, #81954, .F. ) ;
#38114=ORIENTED_EDGE ( 'NONE', *, *, #122546, .T. ) ;
#38115=VERTEX_POINT ( 'NONE', #23528 ) ;
#38118=EDGE_LOOP ( 'NONE', ( #89634, #51915, #74257, #132177 ) ) ;
#38121=VERTEX_POINT ( 'NONE', #69195 ) ;
#38122=LINE ( 'NONE', #113510, #112796 ) ;
#38123=EDGE_CURVE ( 'NONE', #70705, #20468, #91646, .T. ) ;
#38124=ORIENTED_EDGE ( 'NONE', *, *, #129559, .T. ) ;
#38127=DIRECTION ( 'NONE',  ( -0.3543493200069162685, -0.000000000000000000, -0.9351131265310288487 ) ) ;
#38128=ORIENTED_EDGE ( 'NONE', *, *, #116848, .F. ) ;
#38129=ORIENTED_EDGE ( 'NONE', *, *, #130289, .T. ) ;
#38131=DIRECTION ( 'NONE',  ( -0.7071067811865486830, 0.7071067811865464625, 0.000000000000000000 ) ) ;
#38132=DIRECTION ( 'NONE',  ( -0.7071067811865487940, 0.7071067811865463515, 0.000000000000000000 ) ) ;
#38133=ADVANCED_FACE ( 'NONE', ( #113378 ), #35153, .F. ) ;
#38135=EDGE_LOOP ( 'NONE', ( #2269, #35746, #123783, #100918 ) ) ;
#38136=CARTESIAN_POINT ( 'NONE',  ( -26.99999999999980815, 12.25461709320618553, -10.07315571508703478 ) ) ;
#38137=ORIENTED_EDGE ( 'NONE', *, *, #84969, .F. ) ;
#38138=ORIENTED_EDGE ( 'NONE', *, *, #61082, .F. ) ;
#38139=VERTEX_POINT ( 'NONE', #74181 ) ;
#38140=EDGE_LOOP ( 'NONE', ( #20056, #105288, #59501, #9470 ) ) ;
#38141=PLANE ( 'NONE',  #17091 ) ;
#38144=DIRECTION ( 'NONE',  ( -0.7071067811865486830, 0.7071067811865464625, 0.000000000000000000 ) ) ;
#38145=ADVANCED_FACE ( 'NONE', ( #115490 ), #50298, .T. ) ;
#38146=LINE ( 'NONE', #60644, #48347 ) ;
#38147=DIRECTION ( 'NONE',  ( -0.000000000000000000, 0.000000000000000000, 1.000000000000000000 ) ) ;
#38148=ORIENTED_EDGE ( 'NONE', *, *, #58347, .T. ) ;
#38150=DIRECTION ( 'NONE',  ( -0.7071067811865487940, 0.7071067811865463515, 0.000000000000000000 ) ) ;
#38151=AXIS2_PLACEMENT_3D ( 'NONE', #49285, #15167, #35565 ) ;
#38153=DIRECTION ( 'NONE',  ( -0.000000000000000000, -0.3543493200069152693, 0.9351131265310292928 ) ) ;
#38154=DIRECTION ( 'NONE',  ( -0.000000000000000000, 0.000000000000000000, 1.000000000000000000 ) ) ;
#38155=EDGE_CURVE ( 'NONE', #61902, #70075, #107509, .T. ) ;
#38157=ORIENTED_EDGE ( 'NONE', *, *, #86511, .T. ) ;
#38158=VECTOR ( 'NONE', #35177, 1000.000000000000000 ) ;
#38160=ORIENTED_EDGE ( 'NONE', *, *, #136123, .T. ) ;
#38161=FACE_OUTER_BOUND ( 'NONE', #68762, .T. ) ;
#38163=DIRECTION ( 'NONE',  ( -1.000000000000000000, 0.000000000000000000, 0.000000000000000000 ) ) ;
#38165=EDGE_CURVE ( 'NONE', #122527, #82873, #16188, .T. ) ;
#38166=LINE ( 'NONE', #80253, #110764 ) ;
#38170=LINE ( 'NONE', #36712, #34462 ) ;
#38172=DIRECTION ( 'NONE',  ( -0.7071067811865486830, -0.7071067811865464625, 0.000000000000000000 ) ) ;
#38173=DIRECTION ( 'NONE',  ( -0.7071067811865486830, -0.7071067811865464625, -0.000000000000000000 ) ) ;
#38174=CARTESIAN_POINT ( 'NONE',  ( -25.17183060077629619, -17.24070752338409918, 4.000000000000000000 ) ) ;
#38175=ORIENTED_EDGE ( 'NONE', *, *, #18210, .F. ) ;
#38177=VERTEX_POINT ( 'NONE', #28546 ) ;
#38179=CARTESIAN_POINT ( 'NONE',  ( -14.70025512860841133, -27.71228299555195917, 4.000000000000000000 ) ) ;
#38180=CARTESIAN_POINT ( 'NONE',  ( -24.48921356237309510, -27.52281430457072631, 5.000000000000000000 ) ) ;
#38182=DIRECTION ( 'NONE',  ( -0.6830127018922180770, -0.6830127018922204085, -0.2588190451025213501 ) ) ;
#38183=CARTESIAN_POINT ( 'NONE',  ( 5.204170427930421283E-15, -0.4125381241607568028, 4.000000000000000000 ) ) ;
#38184=ORIENTED_EDGE ( 'NONE', *, *, #85869, .F. ) ;
#38185=PLANE ( 'NONE',  #120185 ) ;
#38186=ORIENTED_EDGE ( 'NONE', *, *, #16168, .T. ) ;
#38188=VERTEX_POINT ( 'NONE', #51006 ) ;
#38189=DIRECTION ( 'NONE',  ( -0.7071067811865486830, 0.7071067811865464625, 0.000000000000000000 ) ) ;
#38191=ADVANCED_FACE ( 'NONE', ( #40837 ), #8170, .F. ) ;
#38193=CARTESIAN_POINT ( 'NONE',  ( 0.000000000000000000, 0.000000000000000000, 5.000000000000000000 ) ) ;
#38194=VECTOR ( 'NONE', #126898, 1000.000000000000000 ) ;
#38195=AXIS2_PLACEMENT_3D ( 'NONE', #141149, #20079, #7033 ) ;
#38197=VERTEX_POINT ( 'NONE', #127112 ) ;
#38199=PLANE ( 'NONE',  #65440 ) ;
#38200=CARTESIAN_POINT ( 'NONE',  ( -29.99999999999979750, -13.39766691384885711, -10.96608748226458907 ) ) ;
#38202=DIRECTION ( 'NONE',  ( 0.6830127018922181881, 0.6830127018922202975, -0.2588190451025214056 ) ) ;
#38203=CARTESIAN_POINT ( 'NONE',  ( -18.18398860626898994, 28.73617430169800002, 5.000000000000000000 ) ) ;
#38204=ORIENTED_EDGE ( 'NONE', *, *, #76279, .T. ) ;
#38205=CARTESIAN_POINT ( 'NONE',  ( -6.707106781186494615, -9.740707523384186217, 5.000000000000000000 ) ) ;
#38208=LINE ( 'NONE', #102746, #138079 ) ;
#38209=CARTESIAN_POINT ( 'NONE',  ( 34.92499999999998295, -22.22500000000000142, 4.500000000000000888 ) ) ;
#38210=CARTESIAN_POINT ( 'NONE',  ( 9.299744871391588674, -27.71228299555212971, 4.000000000000000000 ) ) ;
#38211=ORIENTED_EDGE ( 'NONE', *, *, #87590, .F. ) ;
#38212=LINE ( 'NONE', #59275, #134511 ) ;
#38215=CARTESIAN_POINT ( 'NONE',  ( -12.18398860626900060, 28.73617430169795739, 5.000000000000000000 ) ) ;
#38217=DIRECTION ( 'NONE',  ( -0.6830127018922180770, -0.6830127018922204085, -0.2588190451025213501 ) ) ;
#38219=PLANE ( 'NONE',  #97882 ) ;
#38222=EDGE_LOOP ( 'NONE', ( #126170, #65338, #80567, #58013 ) ) ;
#38224=VERTEX_POINT ( 'NONE', #82926 ) ;
#38225=CARTESIAN_POINT ( 'NONE',  ( 27.48921356237309155, -27.52281430457074762, 5.000000000000000000 ) ) ;
#38226=DIRECTION ( 'NONE',  ( -0.000000000000000000, -0.3543493200069152693, 0.9351131265310292928 ) ) ;
#38228=DIRECTION ( 'NONE',  ( 0.6830127018922181881, 0.6830127018922202975, -0.2588190451025214056 ) ) ;
#38229=DIRECTION ( 'NONE',  ( 0.000000000000000000, 1.000000000000000000, 0.000000000000000000 ) ) ;
#38231=CARTESIAN_POINT ( 'NONE',  ( -11.99451991528749417, 28.92564299267946382, 4.000000000000000000 ) ) ;
#38232=DIRECTION ( 'NONE',  ( -0.000000000000000000, 0.3543493200069153248, 0.9351131265310291818 ) ) ;
#38233=ADVANCED_FACE ( 'NONE', ( #72080 ), #85046, .T. ) ;
#38235=DIRECTION ( 'NONE',  ( 0.7071067811865486830, -0.7071067811865464625, -0.000000000000000000 ) ) ;
#38237=DIRECTION ( 'NONE',  ( -0.7071067811865486830, -0.7071067811865464625, -0.000000000000000000 ) ) ;
#38238=ORIENTED_EDGE ( 'NONE', *, *, #72476, .T. ) ;
#38240=ADVANCED_FACE ( 'NONE', ( #105362 ), #51726, .T. ) ;
#38241=CARTESIAN_POINT ( 'NONE',  ( -12.48921356237309155, -27.52281430457064104, 5.000000000000000000 ) ) ;
#38242=ADVANCED_FACE ( 'NONE', ( #117641 ), #19076, .F. ) ;
#38243=EDGE_CURVE ( 'NONE', #3762, #69864, #127868, .T. ) ;
#38245=CARTESIAN_POINT ( 'NONE',  ( -19.82816939922339472, 18.75929247661552779, 4.000000000000000000 ) ) ;
#38246=CARTESIAN_POINT ( 'NONE',  ( -8.999999999999937828, 12.83542986846996570, -1.025386466790349171 ) ) ;
#38248=DIRECTION ( 'NONE',  ( -0.7071067811865486830, 0.7071067811865464625, 0.000000000000000000 ) ) ;
#38249=ADVANCED_FACE ( 'NONE', ( #116959 ), #106784, .T. ) ;
#38250=EDGE_CURVE ( 'NONE', #62679, #32117, #40159, .T. ) ;
#38251=DIRECTION ( 'NONE',  ( 0.6830127018922180770, -0.6830127018922204085, -0.2588190451025213501 ) ) ;
#38252=VECTOR ( 'NONE', #94696, 1000.000000000000000 ) ;
#38253=EDGE_LOOP ( 'NONE', ( #73883, #136570, #24, #45925 ) ) ;
#38254=ORIENTED_EDGE ( 'NONE', *, *, #83411, .F. ) ;
#38255=ORIENTED_EDGE ( 'NONE', *, *, #38097, .F. ) ;
#38256=ADVANCED_FACE ( 'NONE', ( #129250 ), #29938, .F. ) ;
#38257=ORIENTED_EDGE ( 'NONE', *, *, #135081, .F. ) ;
#38258=DIRECTION ( 'NONE',  ( 0.7071067811865486830, -0.7071067811865464625, -0.000000000000000000 ) ) ;
#38259=EDGE_CURVE ( 'NONE', #112794, #132213, #110342, .T. ) ;
#38260=EDGE_LOOP ( 'NONE', ( #125786, #59985, #82868, #64877 ) ) ;
#38261=VECTOR ( 'NONE', #29064, 1000.000000000000000 ) ;
#38262=LINE ( 'NONE', #106326, #28722 ) ;
#38263=LINE ( 'NONE', #128138, #103491 ) ;
#38266=ORIENTED_EDGE ( 'NONE', *, *, #32945, .T. ) ;
#38267=CARTESIAN_POINT ( 'NONE',  ( 33.85005128541003927, -8.240707523384196875, 17.25253755692247282 ) ) ;
#38268=DIRECTION ( 'NONE',  ( -0.7071067811865486830, -0.7071067811865464625, 0.000000000000000000 ) ) ;
#38269=ORIENTED_EDGE ( 'NONE', *, *, #127119, .T. ) ;
#38270=CARTESIAN_POINT ( 'NONE',  ( 5.204170427930421283E-15, -6.412538124160692909, 4.000000000000000000 ) ) ;
#38271=EDGE_LOOP ( 'NONE', ( #78463, #71491, #138918, #141176 ) ) ;
#38272=ORIENTED_EDGE ( 'NONE', *, *, #55216, .T. ) ;
#38273=DIRECTION ( 'NONE',  ( 0.7071067811865487940, -0.7071067811865463515, 0.000000000000000000 ) ) ;
#38274=ORIENTED_EDGE ( 'NONE', *, *, #121811, .F. ) ;
#38275=ORIENTED_EDGE ( 'NONE', *, *, #110847, .F. ) ;
#38277=EDGE_CURVE ( 'NONE', #44302, #66646, #121233, .T. ) ;
#38278=EDGE_LOOP ( 'NONE', ( #9723, #136706, #141934, #7186 ) ) ;
#38279=VECTOR ( 'NONE', #137707, 1000.000000000000000 ) ;
#38283=LINE ( 'NONE', #107088, #79824 ) ;
#38285=CARTESIAN_POINT ( 'NONE',  ( 33.08314806772910543, 21.75929247661549937, 7.311836541448126781 ) ) ;
#38286=AXIS2_PLACEMENT_3D ( 'NONE', #120239, #98528, #119536 ) ;
#38288=EDGE_CURVE ( 'NONE', #58719, #69864, #11740, .T. ) ;
#38289=LINE ( 'NONE', #81090, #48708 ) ;
#38291=PLANE ( 'NONE',  #40058 ) ;
#38292=CARTESIAN_POINT ( 'NONE',  ( 29.29289321881325847, -9.740707523384177335, 5.000000000000000000 ) ) ;
#38293=CARTESIAN_POINT ( 'NONE',  ( 34.42499999999998295, -9.022814304570511368, 5.000000000000000000 ) ) ;
#38294=EDGE_CURVE ( 'NONE', #134932, #89365, #74920, .T. ) ;
#38295=VERTEX_POINT ( 'NONE', #32838 ) ;
#38296=CARTESIAN_POINT ( 'NONE',  ( 0.000000000000000000, 0.000000000000000000, 5.000000000000000000 ) ) ;
#38298=ORIENTED_EDGE ( 'NONE', *, *, #18622, .F. ) ;
#38299=EDGE_CURVE ( 'NONE', #115217, #9024, #135, .T. ) ;
#38300=ORIENTED_EDGE ( 'NONE', *, *, #16802, .T. ) ;
#38301=CARTESIAN_POINT ( 'NONE',  ( -45.29974487139158867, -27.71228299555237840, 4.000000000000000000 ) ) ;
#38303=EDGE_CURVE ( 'NONE', #46717, #133314, #121935, .T. ) ;
#38304=CARTESIAN_POINT ( 'NONE',  ( -13.82816939922343025, -11.24070752338416490, 4.000000000000000000 ) ) ;
#38306=FACE_OUTER_BOUND ( 'NONE', #34669, .T. ) ;
#38307=LINE ( 'NONE', #136179, #97288 ) ;
#38309=ORIENTED_EDGE ( 'NONE', *, *, #14043, .T. ) ;
#38310=CARTESIAN_POINT ( 'NONE',  ( -42.48921356237308800, -27.52281430457085065, 5.000000000000000000 ) ) ;
#38311=ORIENTED_EDGE ( 'NONE', *, *, #71843, .T. ) ;
#38312=EDGE_CURVE ( 'NONE', #106292, #16078, #64021, .T. ) ;
#38313=CARTESIAN_POINT ( 'NONE',  ( -30.18398860626900060, 28.73617430169808173, 5.000000000000000000 ) ) ;
#38315=LINE ( 'NONE', #126718, #114085 ) ;
#38316=CARTESIAN_POINT ( 'NONE',  ( -24.48921356237309510, -27.52281430457072631, 5.000000000000000000 ) ) ;
#38317=EDGE_CURVE ( 'NONE', #45614, #25787, #21926, .T. ) ;
#38318=DIRECTION ( 'NONE',  ( -0.3543493200069162685, -0.000000000000000000, -0.9351131265310288487 ) ) ;
#38319=ORIENTED_EDGE ( 'NONE', *, *, #90990, .T. ) ;
#38320=EDGE_LOOP ( 'NONE', ( #84526, #102675, #116172, #70524 ) ) ;
#38321=EDGE_LOOP ( 'NONE', ( #68185, #58659, #75406 ) ) ;
#38323=CARTESIAN_POINT ( 'NONE',  ( 35.99451991528749772, 28.92564299267963079, 4.000000000000000000 ) ) ;
#38324=CARTESIAN_POINT ( 'NONE',  ( -21.51665438641028771, 22.22500000000000142, 4.500000000000000888 ) ) ;
#38325=DIRECTION ( 'NONE',  ( -0.7071067811865486830, -0.7071067811865464625, 0.000000000000000000 ) ) ;
#38326=LINE ( 'NONE', #27417, #69436 ) ;
#38327=DIRECTION ( 'NONE',  ( -0.000000000000000000, -0.3543493200069152693, 0.9351131265310292928 ) ) ;
#38330=PLANE ( 'NONE',  #21338 ) ;
#38331=ORIENTED_EDGE ( 'NONE', *, *, #122441, .T. ) ;
#38334=ORIENTED_EDGE ( 'NONE', *, *, #5648, .T. ) ;
#38335=DIRECTION ( 'NONE',  ( 0.7071067811865487940, 0.7071067811865463515, 0.000000000000000000 ) ) ;
#38337=ORIENTED_EDGE ( 'NONE', *, *, #78503, .T. ) ;
#38338=EDGE_CURVE ( 'NONE', #41122, #84504, #32099, .T. ) ;
#38339=ORIENTED_EDGE ( 'NONE', *, *, #58467, .F. ) ;
#38340=CARTESIAN_POINT ( 'NONE',  ( 34.92499999999998295, 22.22500000000000142, 4.000000000000000000 ) ) ;
#38341=CARTESIAN_POINT ( 'NONE',  ( 0.000000000000000000, 0.000000000000000000, 5.000000000000000000 ) ) ;
#38342=CARTESIAN_POINT ( 'NONE',  ( 32.24139925780183091, 21.72499999999999432, 5.000000000000000000 ) ) ;
#38343=VERTEX_POINT ( 'NONE', #142308 ) ;
#38344=ORIENTED_EDGE ( 'NONE', *, *, #29068, .T. ) ;
#38345=( BOUNDED_CURVE ( )  B_SPLINE_CURVE ( 3, ( #62359, #127603, #6472, #40601 ),
 .UNSPECIFIED., .F., .T. ) 
 B_SPLINE_CURVE_WITH_KNOTS ( ( 4, 4 ),
 ( 2.779374508378133601, 4.199602562396796301 ),
 .UNSPECIFIED. ) 
 CURVE ( )  GEOMETRIC_REPRESENTATION_ITEM ( )  RATIONAL_B_SPLINE_CURVE ( ( 1.000000000000000000, 0.8388583629366717087, 0.8388583629366717087, 1.000000000000000000 ) ) 
 REPRESENTATION_ITEM ( '' )  );
#38346=CARTESIAN_POINT ( 'NONE',  ( -15.29974487139158867, -27.71228299555216879, 4.000000000000000000 ) ) ;
#38351=CARTESIAN_POINT ( 'NONE',  ( 24.69524342170288023, 1.235879655689124501, 4.000000000000000000 ) ) ;
#38352=CARTESIAN_POINT ( 'NONE',  ( 9.328169399223465774, -0.7407075233842753681, 4.000000000000000000 ) ) ;
#38353=AXIS2_PLACEMENT_3D ( 'NONE', #35219, #50355, #28614 ) ;
#38354=LINE ( 'NONE', #15141, #120856 ) ;
#38355=PLANE ( 'NONE',  #111942 ) ;
#38356=CARTESIAN_POINT ( 'NONE',  ( 0.7928932188134567571, -20.24070752338406720, 5.000000000000000000 ) ) ;
#38359=LINE ( 'NONE', #126767, #96814 ) ;
#38361=DIRECTION ( 'NONE',  ( -1.000000000000000000, -2.666458015092512939E-14, 0.000000000000000000 ) ) ;
#38362=ORIENTED_EDGE ( 'NONE', *, *, #32397, .F. ) ;
#38364=ORIENTED_EDGE ( 'NONE', *, *, #139829, .T. ) ;
#38366=EDGE_CURVE ( 'NONE', #125144, #9222, #46599, .T. ) ;
#38367=EDGE_LOOP ( 'NONE', ( #79097, #132989, #18651, #126741 ) ) ;
#38369=ORIENTED_EDGE ( 'NONE', *, *, #7099, .T. ) ;
#38372=VERTEX_POINT ( 'NONE', #45856 ) ;
#38373=CARTESIAN_POINT ( 'NONE',  ( -21.48921356237309155, -27.52281430457070499, 5.000000000000000000 ) ) ;
#38374=FACE_OUTER_BOUND ( 'NONE', #75061, .T. ) ;
#38377=ADVANCED_FACE ( 'NONE', ( #113208 ), #47997, .F. ) ;
#38378=CARTESIAN_POINT ( 'NONE',  ( 12.70710678118645198, -12.74070752338415247, 5.000000000000000000 ) ) ;
#38379=DIRECTION ( 'NONE',  ( 0.6830127018922180770, -0.6830127018922204085, -0.2588190451025213501 ) ) ;
#38380=LINE ( 'NONE', #125397, #20199 ) ;
#38381=PLANE ( 'NONE',  #142501 ) ;
#38382=CARTESIAN_POINT ( 'NONE',  ( -39.48921356237310221, -27.52281430457082934, 5.000000000000000000 ) ) ;
#38383=LINE ( 'NONE', #84734, #68337 ) ;
#38385=AXIS2_PLACEMENT_3D ( 'NONE', #143227, #132391, #77986 ) ;
#38387=ORIENTED_EDGE ( 'NONE', *, *, #3836, .F. ) ;
#38388=VERTEX_POINT ( 'NONE', #100913 ) ;
#38389=VECTOR ( 'NONE', #111861, 1000.000000000000227 ) ;
#38392=VECTOR ( 'NONE', #114416, 1000.000000000000000 ) ;
#38393=CARTESIAN_POINT ( 'NONE',  ( 30.48921356237309510, -27.52281430457076894, 5.000000000000000000 ) ) ;
#38395=LINE ( 'NONE', #7137, #87441 ) ;
#38396=ORIENTED_EDGE ( 'NONE', *, *, #100152, .T. ) ;
#38397=LINE ( 'NONE', #136269, #88292 ) ;
#38398=CARTESIAN_POINT ( 'NONE',  ( -29.20710678118633297, 3.759292476615681888, 5.000000000000000000 ) ) ;
#38400=ORIENTED_EDGE ( 'NONE', *, *, #14577, .T. ) ;
#38401=FACE_OUTER_BOUND ( 'NONE', #57701, .T. ) ;
#38402=EDGE_CURVE ( 'NONE', #15535, #23113, #112512, .T. ) ;
#38403=EDGE_LOOP ( 'NONE', ( #29368, #41304, #55537, #93281 ) ) ;
#38404=DIRECTION ( 'NONE',  ( 0.7071067811865487940, 0.7071067811865463515, -0.000000000000000000 ) ) ;
#38406=CARTESIAN_POINT ( 'NONE',  ( 0.000000000000000000, 0.000000000000000000, 5.000000000000000000 ) ) ;
#38408=EDGE_LOOP ( 'NONE', ( #29488, #122552 ) ) ;
#38410=ORIENTED_EDGE ( 'NONE', *, *, #124910, .T. ) ;
#38412=EDGE_CURVE ( 'NONE', #97187, #4056, #90784, .T. ) ;
#38413=CARTESIAN_POINT ( 'NONE',  ( 60.18398860626900415, 28.73617430169829490, 5.000000000000000000 ) ) ;
#38416=ADVANCED_FACE ( 'NONE', ( #14627 ), #13169, .T. ) ;
#38417=ADVANCED_FACE ( 'NONE', ( #90032 ), #13880, .T. ) ;
#38418=LINE ( 'NONE', #71064, #98672 ) ;
#38419=EDGE_CURVE ( 'NONE', #75514, #53079, #102375, .T. ) ;
#38421=ORIENTED_EDGE ( 'NONE', *, *, #80517, .F. ) ;
#38422=CARTESIAN_POINT ( 'NONE',  ( 11.99999999999992717, 4.384688058510579189, -7.090945410444659203 ) ) ;
#38423=ADVANCED_FACE ( 'NONE', ( #79219 ), #47316, .F. ) ;
#38424=ORIENTED_EDGE ( 'NONE', *, *, #91524, .T. ) ;
#38427=CARTESIAN_POINT ( 'NONE',  ( -15.32816939922343202, 8.259292476615637923, 4.000000000000000000 ) ) ;
#38429=LINE ( 'NONE', #139188, #136873 ) ;
#38430=PLANE ( 'NONE',  #49586 ) ;
#38431=VERTEX_POINT ( 'NONE', #79932 ) ;
#38432=DIRECTION ( 'NONE',  ( -0.000000000000000000, 0.3543493200069153248, 0.9351131265310292928 ) ) ;
#38437=EDGE_CURVE ( 'NONE', #104032, #73447, #91488, .T. ) ;
#38438=CARTESIAN_POINT ( 'NONE',  ( -20.99451991528748707, 28.92564299267952777, 4.000000000000000000 ) ) ;
#38439=FACE_BOUND ( 'NONE', #125602, .T. ) ;
#38440=VERTEX_POINT ( 'NONE', #138556 ) ;
#38441=DIRECTION ( 'NONE',  ( 0.7071067811865487940, -0.7071067811865463515, 0.000000000000000000 ) ) ;
#38442=CARTESIAN_POINT ( 'NONE',  ( 2.999999999999981792, -6.412538124160691133, 4.000000000000000000 ) ) ;
#38445=PLANE ( 'NONE',  #108277 ) ;
#38446=ORIENTED_EDGE ( 'NONE', *, *, #93622, .F. ) ;
#38447=ORIENTED_EDGE ( 'NONE', *, *, #137560, .T. ) ;
#38448=ADVANCED_FACE ( 'NONE', ( #26925 ), #71174, .F. ) ;
#38449=ORIENTED_EDGE ( 'NONE', *, *, #78486, .T. ) ;
#38450=AXIS2_PLACEMENT_3D ( 'NONE', #140582, #41272, #30415 ) ;
#38452=EDGE_LOOP ( 'NONE', ( #107668, #1048, #111148, #66515, #29106, #118757 ) ) ;
#38453=CARTESIAN_POINT ( 'NONE',  ( -32.99999999999977263, 15.45873954670181938, -0.03131636524286631612 ) ) ;
#38455=PLANE ( 'NONE',  #75192 ) ;
#38458=DIRECTION ( 'NONE',  ( 1.000000000000000000, 0.000000000000000000, 0.000000000000000000 ) ) ;
#38459=CARTESIAN_POINT ( 'NONE',  ( 8.999999999999937828, -18.03360074219755660, 5.000000000000000000 ) ) ;
#38460=PLANE ( 'NONE',  #143194 ) ;
#38461=DIRECTION ( 'NONE',  ( 0.7071067811865487940, 0.7071067811865463515, 0.000000000000000000 ) ) ;
#38463=ORIENTED_EDGE ( 'NONE', *, *, #57389, .F. ) ;
#38465=EDGE_LOOP ( 'NONE', ( #120071, #127971, #132759, #38091 ) ) ;
#38466=ORIENTED_EDGE ( 'NONE', *, *, #8145, .F. ) ;
#38467=ORIENTED_EDGE ( 'NONE', *, *, #119590, .F. ) ;
#38468=ORIENTED_EDGE ( 'NONE', *, *, #94742, .F. ) ;
#38469=EDGE_CURVE ( 'NONE', #40590, #42487, #62938, .T. ) ;
#38471=CARTESIAN_POINT ( 'NONE',  ( -22.49999999999984723, 10.94296225409024537, -9.576120664313309661 ) ) ;
#38472=CARTESIAN_POINT ( 'NONE',  ( -75.18398860626899705, 28.73617430169839793, 5.000000000000000000 ) ) ;
#38474=CARTESIAN_POINT ( 'NONE',  ( 12.27825451568565640, 8.259292476615634371, 11.78515199841153205 ) ) ;
#38475=VERTEX_POINT ( 'NONE', #71894 ) ;
#38477=EDGE_LOOP ( 'NONE', ( #111533, #35013, #78287, #121200 ) ) ;
#38479=VECTOR ( 'NONE', #85811, 1000.000000000000000 ) ;
#38481=CARTESIAN_POINT ( 'NONE',  ( 34.92499999999998295, 8.718490437204167165, 4.759050581649327150 ) ) ;
#38482=AXIS2_PLACEMENT_3D ( 'NONE', #92049, #50706, #137005 ) ;
#38484=ORIENTED_EDGE ( 'NONE', *, *, #104183, .T. ) ;
#38486=LINE ( 'NONE', #27585, #75436 ) ;
#38488=CARTESIAN_POINT ( 'NONE',  ( 45.18398860626900415, 28.73617430169818832, 5.000000000000000000 ) ) ;
#38489=EDGE_CURVE ( 'NONE', #44445, #42198, #18900, .T. ) ;
#38490=CARTESIAN_POINT ( 'NONE',  ( 26.70025512860841488, -27.71228299555187391, 4.000000000000000000 ) ) ;
#38491=VERTEX_POINT ( 'NONE', #48690 ) ;
#38492=ORIENTED_EDGE ( 'NONE', *, *, #131837, .T. ) ;
#38493=LINE ( 'NONE', #82714, #77422 ) ;
#38494=ORIENTED_EDGE ( 'NONE', *, *, #89612, .T. ) ;
#38496=DIRECTION ( 'NONE',  ( -0.000000000000000000, 0.3543493200069153248, 0.9351131265310292928 ) ) ;
#38497=AXIS2_PLACEMENT_3D ( 'NONE', #49262, #136953, #81903 ) ;
#38498=DIRECTION ( 'NONE',  ( 0.7071067811865487940, 0.7071067811865463515, -0.000000000000000000 ) ) ;
#38500=VERTEX_POINT ( 'NONE', #116068 ) ;
#38501=CARTESIAN_POINT ( 'NONE',  ( -33.18398860626899705, 28.73617430169810305, 5.000000000000000000 ) ) ;
#38502=CARTESIAN_POINT ( 'NONE',  ( 24.48921356237309510, -27.52281430457072631, 5.000000000000000000 ) ) ;
#38503=PLANE ( 'NONE',  #83877 ) ;
#38504=ORIENTED_EDGE ( 'NONE', *, *, #14057, .F. ) ;
#38505=LINE ( 'NONE', #105866, #118383 ) ;
#38506=LINE ( 'NONE', #50810, #33191 ) ;
#38507=ORIENTED_EDGE ( 'NONE', *, *, #49867, .F. ) ;
#38508=CARTESIAN_POINT ( 'NONE',  ( 42.18398860626899705, 28.73617430169816700, 5.000000000000000000 ) ) ;
#38509=ORIENTED_EDGE ( 'NONE', *, *, #58939, .F. ) ;
#38510=EDGE_CURVE ( 'NONE', #30925, #14772, #106592, .T. ) ;
#38511=EDGE_CURVE ( 'NONE', #93121, #121113, #82751, .T. ) ;
#38512=VERTEX_POINT ( 'NONE', #126250 ) ;
#38514=ORIENTED_EDGE ( 'NONE', *, *, #138110, .T. ) ;
#38515=CARTESIAN_POINT ( 'NONE',  ( 51.48921356237309510, -27.52281430457091460, 5.000000000000000000 ) ) ;
#38517=CARTESIAN_POINT ( 'NONE',  ( -34.42500000000001137, 17.97718569542923106, 5.000000000000000000 ) ) ;
#38518=ORIENTED_EDGE ( 'NONE', *, *, #117089, .T. ) ;
#38520=CARTESIAN_POINT ( 'NONE',  ( -33.71230993966005940, -21.73547319004781642, 4.999917730833664642 ) ) ;
#38521=DIRECTION ( 'NONE',  ( -0.7071067811865486830, -0.7071067811865464625, 0.000000000000000000 ) ) ;
#38523=DIRECTION ( 'NONE',  ( 0.6830127018922180770, -0.6830127018922204085, -0.2588190451025213501 ) ) ;
#38524=LINE ( 'NONE', #95017, #35139 ) ;
#38525=VECTOR ( 'NONE', #15343, 1000.000000000000000 ) ;
#38526=CARTESIAN_POINT ( 'NONE',  ( 5.816011393731002066, 28.73617430169783304, 5.000000000000000000 ) ) ;
#38528=EDGE_CURVE ( 'NONE', #115259, #124700, #116789, .T. ) ;
#38529=DIRECTION ( 'NONE',  ( -0.000000000000000000, -0.3543493200069152693, 0.9351131265310292928 ) ) ;
#38531=ADVANCED_FACE ( 'NONE', ( #83464 ), #139293, .T. ) ;
#38532=EDGE_LOOP ( 'NONE', ( #5436, #14277, #128183, #72667 ) ) ;
#38533=ORIENTED_EDGE ( 'NONE', *, *, #69838, .T. ) ;
#38535=ADVANCED_FACE ( 'NONE', ( #28373 ), #17471, .F. ) ;
#38536=ORIENTED_EDGE ( 'NONE', *, *, #48782, .F. ) ;
#38537=ORIENTED_EDGE ( 'NONE', *, *, #74661, .F. ) ;
#38538=VERTEX_POINT ( 'NONE', #49435 ) ;
#38539=VECTOR ( 'NONE', #69955, 1000.000000000000000 ) ;
#38541=PLANE ( 'NONE',  #2209 ) ;
#38542=VERTEX_POINT ( 'NONE', #40675 ) ;
#38543=DIRECTION ( 'NONE',  ( 0.7071067811865486830, -0.7071067811865464625, -0.000000000000000000 ) ) ;
#38544=PLANE ( 'NONE',  #74112 ) ;
#38545=DIRECTION ( 'NONE',  ( 0.3543493200069162685, -0.000000000000000000, -0.9351131265310288487 ) ) ;
#38546=FACE_OUTER_BOUND ( 'NONE', #129315, .T. ) ;
#38549=EDGE_CURVE ( 'NONE', #16129, #121292, #93624, .T. ) ;
#38550=DIRECTION ( 'NONE',  ( -0.7071067811865487940, 0.7071067811865463515, -0.000000000000000000 ) ) ;
#38551=CARTESIAN_POINT ( 'NONE',  ( -24.70710678118637205, 5.259292476615659240, 5.000000000000000000 ) ) ;
#38552=CARTESIAN_POINT ( 'NONE',  ( -69.29974487139159578, -27.71228299555254537, 4.000000000000000000 ) ) ;
#38553=CARTESIAN_POINT ( 'NONE',  ( -48.48921356237309510, -27.52281430457089328, 5.000000000000000000 ) ) ;
#38554=FACE_OUTER_BOUND ( 'NONE', #125043, .T. ) ;
#38556=VECTOR ( 'NONE', #76440, 999.9999999999998863 ) ;
#38557=CARTESIAN_POINT ( 'NONE',  ( 4.499999999999962697, -5.568876922607757685, 4.000000000000000000 ) ) ;
#38558=ORIENTED_EDGE ( 'NONE', *, *, #123510, .F. ) ;
#38559=ORIENTED_EDGE ( 'NONE', *, *, #451, .T. ) ;
#38561=AXIS2_PLACEMENT_3D ( 'NONE', #82463, #83171, #104168 ) ;
#38562=ORIENTED_EDGE ( 'NONE', *, *, #101526, .T. ) ;
#38563=LINE ( 'NONE', #92934, #48321 ) ;
#38564=CARTESIAN_POINT ( 'NONE',  ( 24.32816939922336275, 11.25929247661560062, 4.000000000000000000 ) ) ;
#38565=EDGE_LOOP ( 'NONE', ( #18845, #15778, #137760, #47257 ) ) ;
#38566=DIRECTION ( 'NONE',  ( -0.6830127018922180770, -0.6830127018922204085, -0.2588190451025213501 ) ) ;
#38568=PLANE ( 'NONE',  #97579 ) ;
#38569=LINE ( 'NONE', #18950, #134500 ) ;
#38572=ORIENTED_EDGE ( 'NONE', *, *, #58584, .F. ) ;
#38573=CARTESIAN_POINT ( 'NONE',  ( 15.48921356237309510, -27.52281430457066236, 5.000000000000000000 ) ) ;
#38574=VERTEX_POINT ( 'NONE', #128399 ) ;
#38576=DIRECTION ( 'NONE',  ( 0.3543493200069162685, -0.000000000000000000, -0.9351131265310288487 ) ) ;
#38578=CARTESIAN_POINT ( 'NONE',  ( 30.18398860626900060, 28.73617430169808173, 5.000000000000000000 ) ) ;
#38579=EDGE_LOOP ( 'NONE', ( #101857, #57846, #94193, #110149 ) ) ;
#38580=VECTOR ( 'NONE', #74436, 999.9999999999998863 ) ;
#38582=ORIENTED_EDGE ( 'NONE', *, *, #130448, .F. ) ;
#38583=CARTESIAN_POINT ( 'NONE',  ( -8.999999999999932498, 20.70535890316560312, 1.956823837851937142 ) ) ;
#38584=LINE ( 'NONE', #61109, #141121 ) ;
#38585=LINE ( 'NONE', #71960, #24600 ) ;
#38586=DIRECTION ( 'NONE',  ( 0.6830127018922180770, -0.6830127018922204085, -0.2588190451025213501 ) ) ;
#38587=VECTOR ( 'NONE', #32353, 1000.000000000000000 ) ;
#38589=AXIS2_PLACEMENT_3D ( 'NONE', #104875, #60708, #5540 ) ;
#38590=EDGE_CURVE ( 'NONE', #111481, #51650, #29075, .T. ) ;
#38592=EDGE_CURVE ( 'NONE', #141405, #115416, #74013, .T. ) ;
#38593=ORIENTED_EDGE ( 'NONE', *, *, #74351, .F. ) ;
#38594=EDGE_CURVE ( 'NONE', #12864, #59481, #109489, .T. ) ;
#38596=DIRECTION ( 'NONE',  ( -0.3543493200069162685, -0.000000000000000000, -0.9351131265310288487 ) ) ;
#38597=ADVANCED_FACE ( 'NONE', ( #87026 ), #142142, .F. ) ;
#38598=ORIENTED_EDGE ( 'NONE', *, *, #42840, .T. ) ;
#38599=EDGE_LOOP ( 'NONE', ( #32603, #13670, #31014, #54651 ) ) ;
#38601=DIRECTION ( 'NONE',  ( 0.7071067811865486830, -0.7071067811865464625, -0.000000000000000000 ) ) ;
#38602=VERTEX_POINT ( 'NONE', #85577 ) ;
#38603=EDGE_CURVE ( 'NONE', #69752, #54027, #44254, .T. ) ;
#38604=CARTESIAN_POINT ( 'NONE',  ( -62.99451991528749772, 28.92564299267982264, 4.000000000000000000 ) ) ;
#38606=ORIENTED_EDGE ( 'NONE', *, *, #28178, .T. ) ;
#38607=EDGE_CURVE ( 'NONE', #129409, #107840, #129806, .T. ) ;
#38609=ADVANCED_FACE ( 'NONE', ( #74748 ), #119617, .F. ) ;
#38610=FACE_BOUND ( 'NONE', #28270, .T. ) ;
#38612=LINE ( 'NONE', #50209, #54910 ) ;
#38613=DIRECTION ( 'NONE',  ( -0.7071067811865486830, -0.7071067811865464625, -0.000000000000000000 ) ) ;
#38614=ORIENTED_EDGE ( 'NONE', *, *, #88597, .F. ) ;
#38616=LINE ( 'NONE', #16865, #43537 ) ;
#38617=VERTEX_POINT ( 'NONE', #10165 ) ;
#38618=ORIENTED_EDGE ( 'NONE', *, *, #91183, .F. ) ;
#38619=DIRECTION ( 'NONE',  ( 0.3543493200069162685, -0.000000000000000000, -0.9351131265310288487 ) ) ;
#38620=EDGE_CURVE ( 'NONE', #13692, #71393, #87739, .T. ) ;
#38621=EDGE_LOOP ( 'NONE', ( #66517, #41456, #102532, #18469, #111589, #126857 ) ) ;
#38622=VERTEX_POINT ( 'NONE', #32657 ) ;
#38625=ORIENTED_EDGE ( 'NONE', *, *, #75626, .T. ) ;
#38626=CARTESIAN_POINT ( 'NONE',  ( -13.49999999999990763, 7.087461875839172087, 4.000000000000000000 ) ) ;
#38627=PLANE ( 'NONE',  #68184 ) ;
#38628=ORIENTED_EDGE ( 'NONE', *, *, #7147, .T. ) ;
#38630=EDGE_CURVE ( 'NONE', #88501, #97476, #96430, .T. ) ;
#38631=VECTOR ( 'NONE', #110214, 1000.000000000000000 ) ;
#38633=CARTESIAN_POINT ( 'NONE',  ( -12.51665438641036410, 22.22500000000000142, 4.500000000000000888 ) ) ;
#38634=CARTESIAN_POINT ( 'NONE',  ( -0.005480084712502889671, 28.92564299267938210, 4.000000000000000000 ) ) ;
#38636=CARTESIAN_POINT ( 'NONE',  ( -39.18398860626899705, 28.73617430169814568, 5.000000000000000000 ) ) ;
#38637=VERTEX_POINT ( 'NONE', #118927 ) ;
#38638=EDGE_CURVE ( 'NONE', #11170, #118704, #65301, .T. ) ;
#38640=ORIENTED_EDGE ( 'NONE', *, *, #99267, .T. ) ;
#38641=LINE ( 'NONE', #82174, #5613 ) ;
#38642=CARTESIAN_POINT ( 'NONE',  ( 33.48921356237309510, -27.52281430457078670, 5.000000000000000000 ) ) ;
#38643=VERTEX_POINT ( 'NONE', #88469 ) ;
#38644=EDGE_LOOP ( 'NONE', ( #1906, #17047, #31666, #140005 ) ) ;
#38645=ORIENTED_EDGE ( 'NONE', *, *, #76580, .T. ) ;
#38646=DIRECTION ( 'NONE',  ( -0.000000000000000000, 0.3543493200069153248, 0.9351131265310292928 ) ) ;
#38647=AXIS2_PLACEMENT_3D ( 'NONE', #23986, #26828, #57354 ) ;
#38649=EDGE_LOOP ( 'NONE', ( #104791, #78361, #124925, #20546 ) ) ;
#38650=CARTESIAN_POINT ( 'NONE',  ( -32.29289321881322650, 5.259292476615659240, 5.000000000000000000 ) ) ;
#38651=EDGE_CURVE ( 'NONE', #140112, #25422, #19618, .T. ) ;
#38655=DIRECTION ( 'NONE',  ( 1.000000000000000000, 0.000000000000000000, 0.000000000000000000 ) ) ;
#38656=ORIENTED_EDGE ( 'NONE', *, *, #28532, .F. ) ;
#38657=VECTOR ( 'NONE', #100305, 1000.000000000000227 ) ;
#38658=CARTESIAN_POINT ( 'NONE',  ( 0.000000000000000000, 0.000000000000000000, 5.000000000000000000 ) ) ;
#38659=LINE ( 'NONE', #96560, #113670 ) ;
#38660=EDGE_CURVE ( 'NONE', #27268, #126942, #42115, .T. ) ;
#38661=FACE_OUTER_BOUND ( 'NONE', #124710, .T. ) ;
#38662=LINE ( 'NONE', #128532, #116588 ) ;
#38663=ORIENTED_EDGE ( 'NONE', *, *, #142251, .F. ) ;
#38666=CARTESIAN_POINT ( 'NONE',  ( 7.499999999999954703, 22.08746187583901133, 4.000000000000000000 ) ) ;
#38667=CARTESIAN_POINT ( 'NONE',  ( -29.99999999999979039, 7.931123077392108200, 4.000000000000000000 ) ) ;
#38669=ORIENTED_EDGE ( 'NONE', *, *, #54328, .T. ) ;
#38670=EDGE_CURVE ( 'NONE', #6460, #15180, #76895, .T. ) ;
#38671=DIRECTION ( 'NONE',  ( 1.000000000000000000, 0.000000000000000000, 0.000000000000000000 ) ) ;
#38672=DIRECTION ( 'NONE',  ( -0.7071067811865486830, -0.7071067811865464625, 0.000000000000000000 ) ) ;
#38673=PLANE ( 'NONE',  #60707 ) ;
#38674=EDGE_LOOP ( 'NONE', ( #39969, #111531, #35340, #110994 ) ) ;
#38675=CARTESIAN_POINT ( 'NONE',  ( 42.48921356237308800, -27.52281430457085065, 5.000000000000000000 ) ) ;
#38677=LINE ( 'NONE', #57597, #40025 ) ;
#38678=DIRECTION ( 'NONE',  ( 0.7071067811865487940, 0.7071067811865463515, 0.000000000000000000 ) ) ;
#38680=CARTESIAN_POINT ( 'NONE',  ( -51.29974487139158867, -27.71228299555242103, 4.000000000000000000 ) ) ;
#38682=EDGE_CURVE ( 'NONE', #13957, #126797, #110181, .T. ) ;
#38684=VERTEX_POINT ( 'NONE', #42827 ) ;
#38685=DIRECTION ( 'NONE',  ( -0.7071067811865486830, -0.7071067811865464625, -0.000000000000000000 ) ) ;
#38687=AXIS2_PLACEMENT_3D ( 'NONE', #127941, #115569, #5400 ) ;
#38688=VECTOR ( 'NONE', #85642, 1000.000000000000000 ) ;
#38690=FACE_OUTER_BOUND ( 'NONE', #106244, .T. ) ;
#38691=DIRECTION ( 'NONE',  ( 0.7071067811865487940, 0.7071067811865463515, -0.000000000000000000 ) ) ;
#38693=DIRECTION ( 'NONE',  ( 0.7071067811865487940, -0.7071067811865463515, 0.000000000000000000 ) ) ;
#38695=CARTESIAN_POINT ( 'NONE',  ( -18.18398860626898994, 28.73617430169800002, 5.000000000000000000 ) ) ;
#38696=AXIS2_PLACEMENT_3D ( 'NONE', #142687, #141997, #64408 ) ;
#38697=FACE_OUTER_BOUND ( 'NONE', #94294, .T. ) ;
#38699=DIRECTION ( 'NONE',  ( 0.7071067811865487940, 0.7071067811865463515, 0.000000000000000000 ) ) ;
#38701=CARTESIAN_POINT ( 'NONE',  ( 4.828169399223504854, 6.759292476615653023, 4.000000000000000000 ) ) ;
#38702=ORIENTED_EDGE ( 'NONE', *, *, #81716, .F. ) ;
#38704=ADVANCED_FACE ( 'NONE', ( #107339 ), #108736, .F. ) ;
#38705=EDGE_LOOP ( 'NONE', ( #65913, #23715, #130498 ) ) ;
#38706=ORIENTED_EDGE ( 'NONE', *, *, #21840, .F. ) ;
#38707=CARTESIAN_POINT ( 'NONE',  ( 14.20710678118645021, 18.75929247661552068, 5.000000000000000000 ) ) ;
#38708=LINE ( 'NONE', #27825, #110999 ) ;
#38710=DIRECTION ( 'NONE',  ( -0.6830127018922181881, 0.6830127018922202975, -0.2588190451025214056 ) ) ;
#38711=EDGE_CURVE ( 'NONE', #26635, #81537, #75445, .T. ) ;
#38712=LINE ( 'NONE', #19092, #97382 ) ;
#38713=CARTESIAN_POINT ( 'NONE',  ( 36.48921356237310221, -27.52281430457080802, 5.000000000000000000 ) ) ;
#38714=ORIENTED_EDGE ( 'NONE', *, *, #6047, .T. ) ;
#38715=EDGE_CURVE ( 'NONE', #9875, #81835, #86327, .T. ) ;
#38717=FACE_OUTER_BOUND ( 'NONE', #136864, .T. ) ;
#38719=AXIS2_PLACEMENT_3D ( 'NONE', #119045, #110291, #129936 ) ;
#38720=LINE ( 'NONE', #83680, #17721 ) ;
#38721=DIRECTION ( 'NONE',  ( -0.000000000000000000, -0.000000000000000000, 1.000000000000000000 ) ) ;
#38722=FACE_OUTER_BOUND ( 'NONE', #43552, .T. ) ;
#38725=FACE_OUTER_BOUND ( 'NONE', #75362, .T. ) ;
#38726=EDGE_LOOP ( 'NONE', ( #138055, #111813, #137569, #98409 ) ) ;
#38727=ORIENTED_EDGE ( 'NONE', *, *, #74764, .T. ) ;
#38730=CARTESIAN_POINT ( 'NONE',  ( 2.510786437626908008, -27.52281430457053446, 5.000000000000000000 ) ) ;
#38733=VERTEX_POINT ( 'NONE', #92011 ) ;
#38734=ADVANCED_FACE ( 'NONE', ( #67439 ), #23921, .T. ) ;
#38736=DIRECTION ( 'NONE',  ( -0.000000000000000000, -0.3543493200069152693, 0.9351131265310292928 ) ) ;
#38738=VECTOR ( 'NONE', #11578, 1000.000000000000000 ) ;
#38740=EDGE_LOOP ( 'NONE', ( #123792, #23276, #105000, #60656 ) ) ;
#38742=CARTESIAN_POINT ( 'NONE',  ( -12.48921356237309155, -27.52281430457064104, 5.000000000000000000 ) ) ;
#38744=DIRECTION ( 'NONE',  ( -0.000000000000000000, -0.3543493200069152693, 0.9351131265310292928 ) ) ;
#38746=CARTESIAN_POINT ( 'NONE',  ( 11.99999999999992717, -3.412538124160723108, 4.000000000000000000 ) ) ;
#38747=LINE ( 'NONE', #82973, #77683 ) ;
#38748=ORIENTED_EDGE ( 'NONE', *, *, #91721, .T. ) ;
#38749=CARTESIAN_POINT ( 'NONE',  ( -31.49999999999977973, 3.431123077392151277, 4.000000000000000000 ) ) ;
#38750=LINE ( 'NONE', #59120, #66233 ) ;
#38751=LINE ( 'NONE', #117696, #81811 ) ;
#38753=LINE ( 'NONE', #6075, #13687 ) ;
#38754=ORIENTED_EDGE ( 'NONE', *, *, #86746, .F. ) ;
#38756=ORIENTED_EDGE ( 'NONE', *, *, #137173, .T. ) ;
#38757=VECTOR ( 'NONE', #39340, 1000.000000000000000 ) ;
#38758=CARTESIAN_POINT ( 'NONE',  ( 5.994519915287488843, 28.92564299267942118, 4.000000000000000000 ) ) ;
#38759=EDGE_CURVE ( 'NONE', #35892, #9606, #134110, .T. ) ;
#38760=LINE ( 'NONE', #125046, #105 ) ;
#38761=CARTESIAN_POINT ( 'NONE',  ( 28.99806943317882002, -22.22500000000000142, 4.500000000000000888 ) ) ;
#38762=DIRECTION ( 'NONE',  ( 0.7071067811865486830, -0.7071067811865464625, -0.000000000000000000 ) ) ;
#38763=DIRECTION ( 'NONE',  ( 0.3543493200069162685, -0.000000000000000000, -0.9351131265310288487 ) ) ;
#38764=ORIENTED_EDGE ( 'NONE', *, *, #46011, .T. ) ;
#38765=ORIENTED_EDGE ( 'NONE', *, *, #86765, .T. ) ;
#38766=PLANE ( 'NONE',  #51552 ) ;
#38767=DIRECTION ( 'NONE',  ( -0.6830127018922180770, -0.6830127018922204085, -0.2588190451025213501 ) ) ;
#38768=ORIENTED_EDGE ( 'NONE', *, *, #75462, .F. ) ;
#38769=EDGE_CURVE ( 'NONE', #16744, #91733, #56592, .T. ) ;
#38770=EDGE_CURVE ( 'NONE', #131909, #143522, #62202, .T. ) ;
#38771=ORIENTED_EDGE ( 'NONE', *, *, #142510, .T. ) ;
#38772=VECTOR ( 'NONE', #58387, 1000.000000000000000 ) ;
#38773=CARTESIAN_POINT ( 'NONE',  ( 34.47516574401890210, 13.49051761211548772, 4.998110765256834398 ) ) ;
#38774=ORIENTED_EDGE ( 'NONE', *, *, #43223, .F. ) ;
#38779=EDGE_CURVE ( 'NONE', #130625, #130905, #101458, .T. ) ;
#38780=FACE_BOUND ( 'NONE', #140312, .T. ) ;
#38781=ADVANCED_FACE ( 'NONE', ( #80454 ), #78300, .F. ) ;
#38785=EDGE_LOOP ( 'NONE', ( #127120, #68430, #93871, #8344 ) ) ;
#38786=VECTOR ( 'NONE', #129711, 1000.000000000000227 ) ;
#38789=EDGE_CURVE ( 'NONE', #51436, #77362, #12307, .T. ) ;
#38790=VERTEX_POINT ( 'NONE', #112354 ) ;
#38794=ORIENTED_EDGE ( 'NONE', *, *, #36970, .T. ) ;
#38795=CARTESIAN_POINT ( 'NONE',  ( 2.999999999999983569, -3.412538124160724884, 4.000000000000000000 ) ) ;
#38796=AXIS2_PLACEMENT_3D ( 'NONE', #56280, #13409, #22849 ) ;
#38797=CARTESIAN_POINT ( 'NONE',  ( -23.55512991947090029, -0.7407075233842665973, 4.307968247156982677 ) ) ;
#38798=EDGE_CURVE ( 'NONE', #42222, #75919, #2107, .T. ) ;
#38799=LINE ( 'NONE', #138108, #68804 ) ;
#38802=CARTESIAN_POINT ( 'NONE',  ( -2.999999999999975131, -18.41253812416056945, 4.000000000000000000 ) ) ;
#38803=DIRECTION ( 'NONE',  ( -0.6830127018922180770, -0.6830127018922204085, -0.2588190451025213501 ) ) ;
#38804=CARTESIAN_POINT ( 'NONE',  ( 17.99451991528748351, 28.92564299267950645, 4.000000000000000000 ) ) ;
#38807=DIRECTION ( 'NONE',  ( -0.000000000000000000, 0.000000000000000000, 1.000000000000000000 ) ) ;
#38808=CARTESIAN_POINT ( 'NONE',  ( -26.99999999999980105, -13.44781430457069504, 5.000000000000000000 ) ) ;
#38809=ADVANCED_FACE ( 'NONE', ( #89175 ), #1409, .T. ) ;
#38810=CARTESIAN_POINT ( 'NONE',  ( -13.49999999999990408, -12.66682484999667402, -0.6294897503864261834 ) ) ;
#38812=LINE ( 'NONE', #16305, #75009 ) ;
#38813=DIRECTION ( 'NONE',  ( 0.7071067811865486830, -0.7071067811865464625, -0.000000000000000000 ) ) ;
#38814=EDGE_LOOP ( 'NONE', ( #102851, #85486, #42264, #128974 ) ) ;
#38815=ORIENTED_EDGE ( 'NONE', *, *, #127916, .T. ) ;
#38816=ORIENTED_EDGE ( 'NONE', *, *, #29720, .F. ) ;
#38817=ADVANCED_FACE ( 'NONE', ( #133401 ), #122486, .T. ) ;
#38819=AXIS2_PLACEMENT_3D ( 'NONE', #109053, #99600, #143126 ) ;
#38820=EDGE_CURVE ( 'NONE', #135923, #57800, #58005, .T. ) ;
#38821=ORIENTED_EDGE ( 'NONE', *, *, #30562, .T. ) ;
#38822=EDGE_CURVE ( 'NONE', #139365, #119425, #79041, .T. ) ;
#38823=AXIS2_PLACEMENT_3D ( 'NONE', #72422, #60833, #15112 ) ;
#38826=ORIENTED_EDGE ( 'NONE', *, *, #12955, .T. ) ;
#38827=PLANE ( 'NONE',  #128125 ) ;
#38828=ORIENTED_EDGE ( 'NONE', *, *, #16119, .F. ) ;
#38829=PLANE ( 'NONE',  #16375 ) ;
#38831=DIRECTION ( 'NONE',  ( -0.7071067811865487940, 0.7071067811865463515, -0.000000000000000000 ) ) ;
#38833=VERTEX_POINT ( 'NONE', #36913 ) ;
#38834=CARTESIAN_POINT ( 'NONE',  ( -66.29974487139159578, -27.71228299555252406, 4.000000000000000000 ) ) ;
#38835=DIRECTION ( 'NONE',  ( -0.7071067811865487940, 0.7071067811865463515, -0.000000000000000000 ) ) ;
#38837=DIRECTION ( 'NONE',  ( -0.6830127018922180770, -0.6830127018922204085, -0.2588190451025213501 ) ) ;
#38840=EDGE_LOOP ( 'NONE', ( #41253, #102957, #141948, #98545 ) ) ;
#38841=ORIENTED_EDGE ( 'NONE', *, *, #90040, .T. ) ;
#38842=ORIENTED_EDGE ( 'NONE', *, *, #89506, .F. ) ;
#38843=CARTESIAN_POINT ( 'NONE',  ( 34.49999999999975842, 21.43112307739196609, 4.000000000000000000 ) ) ;
#38844=CARTESIAN_POINT ( 'NONE',  ( -35.20003122016815666, 8.259292476615634371, 16.85664084051849443 ) ) ;
#38845=VECTOR ( 'NONE', #99767, 1000.000000000000000 ) ;
#38846=LINE ( 'NONE', #72237, #16956 ) ;
#38847=CARTESIAN_POINT ( 'NONE',  ( -23.99999999999982236, 8.587461875839151659, 4.000000000000000000 ) ) ;
#38848=ORIENTED_EDGE ( 'NONE', *, *, #1737, .T. ) ;
#38851=LINE ( 'NONE', #104813, #28573 ) ;
#38853=CARTESIAN_POINT ( 'NONE',  ( -26.29289321881326913, -3.740707523384244837, 5.000000000000000000 ) ) ;
#38854=DIRECTION ( 'NONE',  ( 0.7071067811865486830, -0.7071067811865464625, -0.000000000000000000 ) ) ;
#38857=ORIENTED_EDGE ( 'NONE', *, *, #60481, .F. ) ;
#38858=ORIENTED_EDGE ( 'NONE', *, *, #25258, .T. ) ;
#38859=EDGE_CURVE ( 'NONE', #123360, #6090, #2854, .T. ) ;
#38860=ORIENTED_EDGE ( 'NONE', *, *, #26350, .T. ) ;
#38861=PLANE ( 'NONE',  #138988 ) ;
#38862=LINE ( 'NONE', #3348, #102097 ) ;
#38864=CARTESIAN_POINT ( 'NONE',  ( 4.499999999999979572, 1.087461875839227154, 4.000000000000000000 ) ) ;
#38865=LINE ( 'NONE', #113544, #52027 ) ;
#38869=CARTESIAN_POINT ( 'NONE',  ( 28.49999999999980815, 14.14708470758593606, -0.5283514160167208651 ) ) ;
#38872=LINE ( 'NONE', #128731, #116155 ) ;
#38873=CARTESIAN_POINT ( 'NONE',  ( -32.99999999999977263, 18.08204922493370148, 0.9627537363045626240 ) ) ;
#38874=ORIENTED_EDGE ( 'NONE', *, *, #18474, .F. ) ;
#38875=CARTESIAN_POINT ( 'NONE',  ( 13.17183060077637968, -20.24070752338407431, 4.000000000000000000 ) ) ;
#38876=ORIENTED_EDGE ( 'NONE', *, *, #5505, .F. ) ;
#38878=LINE ( 'NONE', #84543, #48418 ) ;
#38879=CARTESIAN_POINT ( 'NONE',  ( -10.49999999999992895, -4.796895815301030375, -3.611700055028705503 ) ) ;
#38880=VERTEX_POINT ( 'NONE', #57285 ) ;
#38881=ADVANCED_FACE ( 'NONE', ( #66706 ), #14459, .F. ) ;
#38882=CARTESIAN_POINT ( 'NONE',  ( 0.000000000000000000, 0.000000000000000000, 5.000000000000000000 ) ) ;
#38883=PLANE ( 'NONE',  #77341 ) ;
#38884=EDGE_LOOP ( 'NONE', ( #17859, #83326, #99033, #115561 ) ) ;
#38885=EDGE_CURVE ( 'NONE', #91730, #121313, #126090, .T. ) ;
#38886=ORIENTED_EDGE ( 'NONE', *, *, #80969, .T. ) ;
#38888=EDGE_LOOP ( 'NONE', ( #140523, #113618, #54446, #63117 ) ) ;
#38889=VECTOR ( 'NONE', #140103, 999.9999999999998863 ) ;
#38891=LINE ( 'NONE', #59251, #70485 ) ;
#38893=CARTESIAN_POINT ( 'NONE',  ( -28.49999999999979394, 22.08746187583901843, 4.000000000000000000 ) ) ;
#38895=EDGE_LOOP ( 'NONE', ( #98486, #64528, #130320, #116670 ) ) ;
#38896=EDGE_CURVE ( 'NONE', #56720, #32623, #137685, .T. ) ;
#38897=FACE_OUTER_BOUND ( 'NONE', #71047, .T. ) ;
#38898=CARTESIAN_POINT ( 'NONE',  ( 0.4892135623730947680, -27.52281430457055578, 5.000000000000000000 ) ) ;
#38901=LINE ( 'NONE', #83124, #116195 ) ;
#38902=ORIENTED_EDGE ( 'NONE', *, *, #26113, .F. ) ;
#38903=EDGE_CURVE ( 'NONE', #127446, #19682, #39809, .T. ) ;
#38905=VERTEX_POINT ( 'NONE', #105027 ) ;
#38907=DIRECTION ( 'NONE',  ( -0.6830127018922180770, -0.6830127018922204085, -0.2588190451025213501 ) ) ;
#38908=DIRECTION ( 'NONE',  ( 0.7071067811865487940, 0.7071067811865463515, -0.000000000000000000 ) ) ;
#38909=CARTESIAN_POINT ( 'NONE',  ( -10.17183060077639389, -11.24070752338416845, 4.000000000000000000 ) ) ;
#38910=VERTEX_POINT ( 'NONE', #105716 ) ;
#38911=EDGE_CURVE ( 'NONE', #16679, #24719, #38359, .T. ) ;
#38912=EDGE_CURVE ( 'NONE', #70384, #114250, #92716, .T. ) ;
#38913=LINE ( 'NONE', #4795, #72077 ) ;
#38914=VECTOR ( 'NONE', #121191, 1000.000000000000227 ) ;
#38915=DIRECTION ( 'NONE',  ( -0.7071067811865487940, 0.7071067811865463515, 0.000000000000000000 ) ) ;
#38916=LINE ( 'NONE', #106271, #2212 ) ;
#38917=FACE_OUTER_BOUND ( 'NONE', #3881, .T. ) ;
#38918=DIRECTION ( 'NONE',  ( 0.7071067811865487940, -0.7071067811865463515, 0.000000000000000000 ) ) ;
#38920=CARTESIAN_POINT ( 'NONE',  ( -20.66652290003515446, 8.920938975803856863, 4.000000000000000000 ) ) ;
#38921=VECTOR ( 'NONE', #99391, 999.9999999999998863 ) ;
#38922=LINE ( 'NONE', #28772, #19839 ) ;
#38925=ORIENTED_EDGE ( 'NONE', *, *, #76754, .T. ) ;
#38926=ORIENTED_EDGE ( 'NONE', *, *, #825, .F. ) ;
#38928=VERTEX_POINT ( 'NONE', #9061 ) ;
#38929=DIRECTION ( 'NONE',  ( 0.7071067811865487940, -0.7071067811865463515, 0.000000000000000000 ) ) ;
#38930=EDGE_CURVE ( 'NONE', #130643, #118381, #27449, .T. ) ;
#38931=CARTESIAN_POINT ( 'NONE',  ( 17.51078643762690845, -27.52281430457043143, 5.000000000000000000 ) ) ;
#38932=CARTESIAN_POINT ( 'NONE',  ( 45.18398860626900415, 28.73617430169818832, 5.000000000000000000 ) ) ;
#38933=CARTESIAN_POINT ( 'NONE',  ( -21.48921356237309155, -27.52281430457070499, 5.000000000000000000 ) ) ;
#38935=VECTOR ( 'NONE', #87321, 1000.000000000000114 ) ;
#38936=DIRECTION ( 'NONE',  ( 0.7071067811865487940, 0.7071067811865463515, 0.000000000000000000 ) ) ;
#38937=CARTESIAN_POINT ( 'NONE',  ( -5.953411863704523022, 14.25929247661556332, 18.84478104361329187 ) ) ;
#38938=VECTOR ( 'NONE', #40322, 1000.000000000000000 ) ;
#38939=EDGE_CURVE ( 'NONE', #101265, #139589, #84034, .T. ) ;
#38941=ORIENTED_EDGE ( 'NONE', *, *, #40711, .F. ) ;
#38942=CARTESIAN_POINT ( 'NONE',  ( 2.999999999999987121, 7.552185695429095347, 5.000000000000000000 ) ) ;
#38944=DIRECTION ( 'NONE',  ( 0.7071067811865487940, 0.7071067811865463515, 0.000000000000000000 ) ) ;
#38945=EDGE_CURVE ( 'NONE', #116931, #26300, #49260, .T. ) ;
#38946=EDGE_LOOP ( 'NONE', ( #10667, #135995, #6751, #171 ) ) ;
#38947=ORIENTED_EDGE ( 'NONE', *, *, #3543, .T. ) ;
#38948=EDGE_CURVE ( 'NONE', #39146, #118497, #42491, .T. ) ;
#38949=EDGE_CURVE ( 'NONE', #62934, #10446, #28194, .T. ) ;
#38950=LINE ( 'NONE', #73040, #80183 ) ;
#38951=DIRECTION ( 'NONE',  ( -0.6830127018922181881, 0.6830127018922202975, -0.2588190451025214056 ) ) ;
#38952=LINE ( 'NONE', #83922, #90497 ) ;
#38953=DIRECTION ( 'NONE',  ( -0.7071067811865487940, 0.7071067811865463515, -0.000000000000000000 ) ) ;
#38955=CARTESIAN_POINT ( 'NONE',  ( -34.92500000000001137, 21.72500000000000142, 5.000000000000000000 ) ) ;
#38956=VERTEX_POINT ( 'NONE', #139107 ) ;
#38957=ORIENTED_EDGE ( 'NONE', *, *, #66263, .F. ) ;
#38959=ORIENTED_EDGE ( 'NONE', *, *, #85649, .F. ) ;
#38960=EDGE_CURVE ( 'NONE', #5368, #42711, #48514, .T. ) ;
#38961=ORIENTED_EDGE ( 'NONE', *, *, #38770, .T. ) ;
#38962=EDGE_CURVE ( 'NONE', #29861, #86656, #17305, .T. ) ;
#38964=EDGE_LOOP ( 'NONE', ( #66867, #37299, #90035, #61409 ) ) ;
#38965=LINE ( 'NONE', #51287, #61152 ) ;
#38966=LINE ( 'NONE', #7002, #115066 ) ;
#38968=AXIS2_PLACEMENT_3D ( 'NONE', #43269, #76622, #32385 ) ;
#38969=VECTOR ( 'NONE', #37972, 1000.000000000000227 ) ;
#38970=DIRECTION ( 'NONE',  ( -0.7071067811865486830, -0.7071067811865464625, 0.000000000000000000 ) ) ;
#38972=CARTESIAN_POINT ( 'NONE',  ( -11.99999999999991473, -1.447814304570815169, 5.000000000000000000 ) ) ;
#38973=DIRECTION ( 'NONE',  ( -1.000000000000000000, 0.000000000000000000, 0.000000000000000000 ) ) ;
#38974=VECTOR ( 'NONE', #74089, 1000.000000000000000 ) ;
#38975=EDGE_LOOP ( 'NONE', ( #70511, #131105, #37866, #4709 ) ) ;
#38976=DIRECTION ( 'NONE',  ( -0.6830127018922180770, -0.6830127018922204085, -0.2588190451025213501 ) ) ;
#38978=VERTEX_POINT ( 'NONE', #136950 ) ;
#38979=DIRECTION ( 'NONE',  ( -1.000000000000000000, 0.000000000000000000, 0.000000000000000000 ) ) ;
#38980=EDGE_LOOP ( 'NONE', ( #4825, #2540, #19496, #97958 ) ) ;
#38981=ORIENTED_EDGE ( 'NONE', *, *, #130232, .F. ) ;
#38983=VECTOR ( 'NONE', #88404, 1000.000000000000000 ) ;
#38985=VECTOR ( 'NONE', #94233, 999.9999999999998863 ) ;
#38986=EDGE_CURVE ( 'NONE', #121050, #109497, #4956, .T. ) ;
#38987=PLANE ( 'NONE',  #32710 ) ;
#38989=CARTESIAN_POINT ( 'NONE',  ( -18.29974487139159223, -27.71228299555219010, 4.000000000000000000 ) ) ;
#38991=CARTESIAN_POINT ( 'NONE',  ( -5.816011393731002066, 28.73617430169783304, 5.000000000000000000 ) ) ;
#38994=CARTESIAN_POINT ( 'NONE',  ( -12.77004279457784186, 21.73644205237998150, 5.000000000000000888 ) ) ;
#38996=EDGE_CURVE ( 'NONE', #43627, #121003, #70320, .T. ) ;
#38997=CARTESIAN_POINT ( 'NONE',  ( -30.70710678118632586, -18.74070752338408852, 5.000000000000000000 ) ) ;
#38998=( BOUNDED_CURVE ( )  B_SPLINE_CURVE ( 3, ( #99538, #2355, #46670, #88712 ),
 .UNSPECIFIED., .F., .F. ) 
 B_SPLINE_CURVE_WITH_KNOTS ( ( 4, 4 ),
 ( 4.350170835173024386, 4.500739107949268458 ),
 .UNSPECIFIED. ) 
 CURVE ( )  GEOMETRIC_REPRESENTATION_ITEM ( )  RATIONAL_B_SPLINE_CURVE ( ( 1.000000000000000000, 0.9981116584018941973, 0.9981116584018941973, 1.000000000000000000 ) ) 
 REPRESENTATION_ITEM ( '' )  );
#38999=LINE ( 'NONE', #27381, #28201 ) ;
#39000=LINE ( 'NONE', #112979, #6570 ) ;
#39002=VECTOR ( 'NONE', #29591, 1000.000000000000227 ) ;
#39005=ORIENTED_EDGE ( 'NONE', *, *, #37304, .F. ) ;
#39006=ORIENTED_EDGE ( 'NONE', *, *, #116514, .F. ) ;
#39007=VECTOR ( 'NONE', #71711, 1000.000000000000000 ) ;
#39009=ORIENTED_EDGE ( 'NONE', *, *, #103869, .F. ) ;
#39011=FACE_OUTER_BOUND ( 'NONE', #118016, .T. ) ;
#39013=VECTOR ( 'NONE', #91943, 1000.000000000000227 ) ;
#39015=DIRECTION ( 'NONE',  ( -0.000000000000000000, 0.000000000000000000, 1.000000000000000000 ) ) ;
#39016=ORIENTED_EDGE ( 'NONE', *, *, #22193, .T. ) ;
#39017=VERTEX_POINT ( 'NONE', #117311 ) ;
#39019=CARTESIAN_POINT ( 'NONE',  ( -15.00548008471250228, 28.92564299267927552, 4.000000000000000000 ) ) ;
#39021=CARTESIAN_POINT ( 'NONE',  ( -45.48921356237309510, -27.52281430457087197, 5.000000000000000000 ) ) ;
#39022=ORIENTED_EDGE ( 'NONE', *, *, #114951, .F. ) ;
#39023=VERTEX_POINT ( 'NONE', #81901 ) ;
#39024=EDGE_LOOP ( 'NONE', ( #74966, #132758, #72584, #41298 ) ) ;
#39027=PLANE ( 'NONE',  #35833 ) ;
#39028=VECTOR ( 'NONE', #53242, 1000.000000000000000 ) ;
#39031=VECTOR ( 'NONE', #33558, 999.9999999999998863 ) ;
#39032=LINE ( 'NONE', #37624, #48052 ) ;
#39034=PLANE ( 'NONE',  #2617 ) ;
#39035=FACE_OUTER_BOUND ( 'NONE', #76707, .T. ) ;
#39036=VERTEX_POINT ( 'NONE', #15146 ) ;
#39037=CARTESIAN_POINT ( 'NONE',  ( 2.994519915287485734, 28.92564299267940342, 4.000000000000000000 ) ) ;
#39038=PLANE ( 'NONE',  #5391 ) ;
#39039=VERTEX_POINT ( 'NONE', #59427 ) ;
#39041=LINE ( 'NONE', #82551, #94659 ) ;
#39043=ORIENTED_EDGE ( 'NONE', *, *, #118824, .T. ) ;
#39044=EDGE_CURVE ( 'NONE', #49517, #23600, #130920, .T. ) ;
#39045=EDGE_CURVE ( 'NONE', #90465, #31526, #1755, .T. ) ;
#39046=DIRECTION ( 'NONE',  ( -1.000000000000000000, 0.000000000000000000, -0.000000000000000000 ) ) ;
#39047=CARTESIAN_POINT ( 'NONE',  ( 34.92499999999998295, -1.545334305399975072, 14.00746825007384899 ) ) ;
#39048=VERTEX_POINT ( 'NONE', #101108 ) ;
#39049=CARTESIAN_POINT ( 'NONE',  ( -2.999999999999978240, 2.966399257802228906, 5.000000000000000000 ) ) ;
#39051=ORIENTED_EDGE ( 'NONE', *, *, #15205, .F. ) ;
#39052=EDGE_CURVE ( 'NONE', #45045, #16291, #131621, .T. ) ;
#39053=EDGE_CURVE ( 'NONE', #16596, #118999, #100419, .T. ) ;
#39055=DIRECTION ( 'NONE',  ( 0.7071067811865486830, -0.7071067811865464625, -0.000000000000000000 ) ) ;
#39057=CARTESIAN_POINT ( 'NONE',  ( 29.99999999999979394, 10.93112307739207623, 4.000000000000000000 ) ) ;
#39058=CARTESIAN_POINT ( 'NONE',  ( 12.00548008471251293, 28.92564299267929684, 4.000000000000000000 ) ) ;
#39060=DIRECTION ( 'NONE',  ( 1.000000000000000000, 0.000000000000000000, 0.000000000000000000 ) ) ;
#39061=CARTESIAN_POINT ( 'NONE',  ( -5.345055162546144878, 5.259292476615662792, 12.77922209995892722 ) ) ;
#39062=LINE ( 'NONE', #50649, #18181 ) ;
#39065=DIRECTION ( 'NONE',  ( 0.3543493200069162685, -0.000000000000000000, -0.9351131265310288487 ) ) ;
#39066=LINE ( 'NONE', #128232, #7306 ) ;
#39067=CARTESIAN_POINT ( 'NONE',  ( -25.49999999999982947, -4.216083040037277740, -7.486842126848599399 ) ) ;
#39068=ORIENTED_EDGE ( 'NONE', *, *, #128054, .T. ) ;
#39069=ORIENTED_EDGE ( 'NONE', *, *, #101494, .F. ) ;
#39071=ADVANCED_FACE ( 'NONE', ( #31592 ), #78662, .F. ) ;
#39072=CYLINDRICAL_SURFACE ( 'NONE', #130034, 0.5000000000000004441 ) ;
#39073=ORIENTED_EDGE ( 'NONE', *, *, #110008, .T. ) ;
#39074=ORIENTED_EDGE ( 'NONE', *, *, #99601, .F. ) ;
#39075=CARTESIAN_POINT ( 'NONE',  ( 11.28242261357426202, -21.73023691814493930, 5.000000000000000888 ) ) ;
#39076=CARTESIAN_POINT ( 'NONE',  ( -10.41009064519825955, 9.759292476615618384, 11.28811694763776430 ) ) ;
#39078=ORIENTED_EDGE ( 'NONE', *, *, #46480, .F. ) ;
#39081=AXIS2_PLACEMENT_3D ( 'NONE', #16348, #94639, #72247 ) ;
#39083=DIRECTION ( 'NONE',  ( -0.7071067811865487940, 0.7071067811865463515, 0.000000000000000000 ) ) ;
#39085=VECTOR ( 'NONE', #62342, 1000.000000000000227 ) ;
#39086=LINE ( 'NONE', #139852, #55655 ) ;
#39087=DIRECTION ( 'NONE',  ( 0.7071067811865487940, 0.7071067811865463515, 0.000000000000000000 ) ) ;
#39088=DIRECTION ( 'NONE',  ( -0.000000000000000000, 0.000000000000000000, 1.000000000000000000 ) ) ;
#39089=CARTESIAN_POINT ( 'NONE',  ( -24.30132219248945447, 6.014229859109025966, 4.331046227559734341 ) ) ;
#39090=ADVANCED_FACE ( 'NONE', ( #120714 ), #110539, .T. ) ;
#39091=VECTOR ( 'NONE', #78238, 1000.000000000000000 ) ;
#39092=DIRECTION ( 'NONE',  ( -0.7071067811865487940, 0.7071067811865463515, -0.000000000000000000 ) ) ;
#39093=DIRECTION ( 'NONE',  ( -0.000000000000000000, 0.3543493200069153248, 0.9351131265310292928 ) ) ;
#39094=CARTESIAN_POINT ( 'NONE',  ( 5.816011393731002066, 28.73617430169783304, 5.000000000000000000 ) ) ;
#39095=VECTOR ( 'NONE', #56905, 1000.000000000000000 ) ;
#39096=CARTESIAN_POINT ( 'NONE',  ( -30.18398860626900060, 28.73617430169808173, 5.000000000000000000 ) ) ;
#39097=DIRECTION ( 'NONE',  ( 0.3543493200069162685, -0.000000000000000000, -0.9351131265310288487 ) ) ;
#39098=ORIENTED_EDGE ( 'NONE', *, *, #41306, .F. ) ;
#39099=VERTEX_POINT ( 'NONE', #33750 ) ;
#39101=ORIENTED_EDGE ( 'NONE', *, *, #25375, .T. ) ;
#39102=EDGE_CURVE ( 'NONE', #62405, #68775, #122138, .T. ) ;
#39103=CARTESIAN_POINT ( 'NONE',  ( -29.03689333454773447, -22.22500000000000142, 7.231223724525455587 ) ) ;
#39104=VECTOR ( 'NONE', #12290, 1000.000000000000000 ) ;
#39105=CARTESIAN_POINT ( 'NONE',  ( 4.828169399223495084, -8.240707523384200428, 4.000000000000000000 ) ) ;
#39106=ORIENTED_EDGE ( 'NONE', *, *, #10481, .F. ) ;
#39107=DIRECTION ( 'NONE',  ( -0.3543493200069162685, -0.000000000000000000, -0.9351131265310288487 ) ) ;
#39108=FACE_OUTER_BOUND ( 'NONE', #31622, .T. ) ;
#39109=ADVANCED_FACE ( 'NONE', ( #10519 ), #11213, .F. ) ;
#39110=VECTOR ( 'NONE', #130201, 1000.000000000000227 ) ;
#39112=ORIENTED_EDGE ( 'NONE', *, *, #81065, .F. ) ;
#39115=VERTEX_POINT ( 'NONE', #11953 ) ;
#39116=DIRECTION ( 'NONE',  ( 0.7071067811865487940, 0.7071067811865463515, -0.000000000000000000 ) ) ;
#39117=VECTOR ( 'NONE', #62435, 999.9999999999998863 ) ;
#39118=DIRECTION ( 'NONE',  ( -0.7071067811865487940, 0.7071067811865463515, -0.000000000000000000 ) ) ;
#39119=CARTESIAN_POINT ( 'NONE',  ( 30.18398860626900060, 28.73617430169808173, 5.000000000000000000 ) ) ;
#39121=LINE ( 'NONE', #24848, #32357 ) ;
#39122=VECTOR ( 'NONE', #63678, 1000.000000000000000 ) ;
#39123=EDGE_CURVE ( 'NONE', #102268, #65177, #27760, .T. ) ;
#39124=VECTOR ( 'NONE', #100563, 1000.000000000000000 ) ;
#39125=EDGE_LOOP ( 'NONE', ( #27981, #44466, #51984, #60633 ) ) ;
#39126=ORIENTED_EDGE ( 'NONE', *, *, #73769, .T. ) ;
#39127=VERTEX_POINT ( 'NONE', #45351 ) ;
#39128=DIRECTION ( 'NONE',  ( -0.6830127018922180770, -0.6830127018922204085, -0.2588190451025213501 ) ) ;
#39129=LINE ( 'NONE', #40562, #73140 ) ;
#39131=VECTOR ( 'NONE', #91329, 1000.000000000000114 ) ;
#39132=AXIS2_PLACEMENT_3D ( 'NONE', #134596, #2607, #48271 ) ;
#39133=DIRECTION ( 'NONE',  ( 0.7071067811865487940, -0.7071067811865463515, 0.000000000000000000 ) ) ;
#39134=CARTESIAN_POINT ( 'NONE',  ( -31.99806943317879515, -22.22500000000000142, 4.500000000000000888 ) ) ;
#39135=ORIENTED_EDGE ( 'NONE', *, *, #31383, .F. ) ;
#39136=ORIENTED_EDGE ( 'NONE', *, *, #25430, .F. ) ;
#39137=EDGE_CURVE ( 'NONE', #125282, #129157, #98277, .T. ) ;
#39138=DIRECTION ( 'NONE',  ( -0.7071067811865486830, 0.7071067811865464625, 0.000000000000000000 ) ) ;
#39139=ORIENTED_EDGE ( 'NONE', *, *, #99401, .F. ) ;
#39141=VECTOR ( 'NONE', #128704, 1000.000000000000000 ) ;
#39142=EDGE_CURVE ( 'NONE', #93894, #102448, #54780, .T. ) ;
#39144=CARTESIAN_POINT ( 'NONE',  ( 31.82816939922330235, -5.240707523384235955, 4.000000000000000000 ) ) ;
#39145=FACE_OUTER_BOUND ( 'NONE', #44644, .T. ) ;
#39146=VERTEX_POINT ( 'NONE', #114133 ) ;
#39147=LINE ( 'NONE', #83364, #127019 ) ;
#39148=DIRECTION ( 'NONE',  ( 0.000000000000000000, 0.000000000000000000, 1.000000000000000000 ) ) ;
#39149=LINE ( 'NONE', #72537, #62921 ) ;
#39150=ORIENTED_EDGE ( 'NONE', *, *, #5477, .F. ) ;
#39151=LINE ( 'NONE', #38438, #141406 ) ;
#39152=FACE_BOUND ( 'NONE', #55958, .T. ) ;
#39154=LINE ( 'NONE', #47914, #52704 ) ;
#39155=CARTESIAN_POINT ( 'NONE',  ( -25.49999999999981526, 0.4497235411627213963, -5.599840258123600201 ) ) ;
#39156=CARTESIAN_POINT ( 'NONE',  ( 6.299744871391586898, -27.71228299555210484, 4.000000000000000000 ) ) ;
#39159=LINE ( 'NONE', #52164, #85232 ) ;
#39160=VERTEX_POINT ( 'NONE', #137331 ) ;
#39161=ORIENTED_EDGE ( 'NONE', *, *, #31476, .T. ) ;
#39162=ORIENTED_EDGE ( 'NONE', *, *, #57506, .T. ) ;
#39165=EDGE_LOOP ( 'NONE', ( #64537, #56195, #59287, #46430 ) ) ;
#39166=FACE_OUTER_BOUND ( 'NONE', #87001, .T. ) ;
#39167=CARTESIAN_POINT ( 'NONE',  ( -11.99999999999990230, -16.44781430457067373, 5.000000000000000000 ) ) ;
#39169=LINE ( 'NONE', #127608, #96839 ) ;
#39170=EDGE_CURVE ( 'NONE', #93730, #16801, #35178, .T. ) ;
#39171=DIRECTION ( 'NONE',  ( 0.3543493200069162685, -0.000000000000000000, -0.9351131265310288487 ) ) ;
#39172=ADVANCED_FACE ( 'NONE', ( #24963 ), #135210, .F. ) ;
#39173=FACE_OUTER_BOUND ( 'NONE', #28200, .T. ) ;
#39174=FACE_OUTER_BOUND ( 'NONE', #70132, .T. ) ;
#39175=CARTESIAN_POINT ( 'NONE',  ( 24.04658813629530201, 14.25929247661557042, 18.84478104361322082 ) ) ;
#39176=ORIENTED_EDGE ( 'NONE', *, *, #115171, .F. ) ;
#39177=ORIENTED_EDGE ( 'NONE', *, *, #5362, .F. ) ;
#39179=ORIENTED_EDGE ( 'NONE', *, *, #85632, .T. ) ;
#39180=VERTEX_POINT ( 'NONE', #59087 ) ;
#39181=CARTESIAN_POINT ( 'NONE',  ( -28.17183060077627133, 18.75929247661552424, 4.000000000000000000 ) ) ;
#39182=VECTOR ( 'NONE', #62710, 1000.000000000000000 ) ;
#39186=VECTOR ( 'NONE', #90503, 1000.000000000000000 ) ;
#39187=EDGE_LOOP ( 'NONE', ( #132546, #123905, #47896, #84495 ) ) ;
#39188=LINE ( 'NONE', #105145, #37558 ) ;
#39189=CARTESIAN_POINT ( 'NONE',  ( 4.499999999999972466, -4.533600742197694267, 5.000000000000000000 ) ) ;
#39190=EDGE_CURVE ( 'NONE', #35605, #68587, #103941, .T. ) ;
#39191=CARTESIAN_POINT ( 'NONE',  ( 8.999999999999944933, 2.966399257802236011, 5.000000000000000000 ) ) ;
#39192=ORIENTED_EDGE ( 'NONE', *, *, #45285, .F. ) ;
#39193=PLANE ( 'NONE',  #11673 ) ;
#39194=ORIENTED_EDGE ( 'NONE', *, *, #109442, .F. ) ;
#39195=( BOUNDED_CURVE ( )  B_SPLINE_CURVE ( 3, ( #117876, #41077, #50533, #104904 ),
 .UNSPECIFIED., .F., .T. ) 
 B_SPLINE_CURVE_WITH_KNOTS ( ( 4, 4 ),
 ( 0.9743798061614656891, 1.027697802963069451 ),
 .UNSPECIFIED. ) 
 CURVE ( )  GEOMETRIC_REPRESENTATION_ITEM ( )  RATIONAL_B_SPLINE_CURVE ( ( 1.000000000000000000, 0.9997631132982454094, 0.9997631132982454094, 1.000000000000000000 ) ) 
 REPRESENTATION_ITEM ( '' )  );
#39196=DIRECTION ( 'NONE',  ( 0.7071067811865487940, -0.7071067811865463515, 0.000000000000000000 ) ) ;
#39198=ORIENTED_EDGE ( 'NONE', *, *, #106994, .T. ) ;
#39200=CARTESIAN_POINT ( 'NONE',  ( 29.99999999999978684, 4.965500833774356693, -4.007596771432726079 ) ) ;
#39205=CARTESIAN_POINT ( 'NONE',  ( 34.92499999999998295, 22.22500000000000142, 4.000000000000000000 ) ) ;
#39206=ORIENTED_EDGE ( 'NONE', *, *, #60664, .T. ) ;
#39207=AXIS2_PLACEMENT_3D ( 'NONE', #4766, #114968, #59247 ) ;
#39209=DIRECTION ( 'NONE',  ( -0.7071067811865486830, -0.7071067811865464625, -0.000000000000000000 ) ) ;
#39211=DIRECTION ( 'NONE',  ( -0.000000000000000000, -0.3543493200069152693, 0.9351131265310292928 ) ) ;
#39212=CARTESIAN_POINT ( 'NONE',  ( -25.17183060077628909, 3.759292476615678336, 4.000000000000000000 ) ) ;
#39213=ORIENTED_EDGE ( 'NONE', *, *, #6615, .F. ) ;
#39215=VECTOR ( 'NONE', #45186, 1000.000000000000000 ) ;
#39216=FACE_OUTER_BOUND ( 'NONE', #18031, .T. ) ;
#39217=PLANE ( 'NONE',  #107008 ) ;
#39218=EDGE_CURVE ( 'NONE', #141554, #100356, #57433, .T. ) ;
#39219=ORIENTED_EDGE ( 'NONE', *, *, #24998, .T. ) ;
#39220=DIRECTION ( 'NONE',  ( -0.7071067811865486830, 0.7071067811865464625, 0.000000000000000000 ) ) ;
#39221=VECTOR ( 'NONE', #138622, 1000.000000000000000 ) ;
#39222=CARTESIAN_POINT ( 'NONE',  ( 14.99999999999989519, 17.96639925780207747, 5.000000000000000000 ) ) ;
#39223=EDGE_CURVE ( 'NONE', #70988, #41423, #59775, .T. ) ;
#39224=ORIENTED_EDGE ( 'NONE', *, *, #1291, .F. ) ;
#39225=VECTOR ( 'NONE', #96422, 1000.000000000000000 ) ;
#39226=FACE_OUTER_BOUND ( 'NONE', #116181, .T. ) ;
#39227=ORIENTED_EDGE ( 'NONE', *, *, #60740, .F. ) ;
#39229=EDGE_CURVE ( 'NONE', #29394, #50127, #60502, .T. ) ;
#39232=AXIS2_PLACEMENT_3D ( 'NONE', #20860, #107856, #75281 ) ;
#39233=DIRECTION ( 'NONE',  ( 0.7071067811865487940, 0.7071067811865463515, 0.000000000000000000 ) ) ;
#39234=ORIENTED_EDGE ( 'NONE', *, *, #95227, .F. ) ;
#39235=CARTESIAN_POINT ( 'NONE',  ( 81.29974487139159578, -27.71228299555262709, 4.000000000000000000 ) ) ;
#39237=EDGE_CURVE ( 'NONE', #16172, #28113, #90235, .T. ) ;
#39238=EDGE_CURVE ( 'NONE', #58071, #44292, #57645, .T. ) ;
#39239=DIRECTION ( 'NONE',  ( -0.3543493200069162685, -0.000000000000000000, -0.9351131265310288487 ) ) ;
#39240=PLANE ( 'NONE',  #113274 ) ;
#39241=EDGE_CURVE ( 'NONE', #134483, #23024, #125745, .T. ) ;
#39242=ORIENTED_EDGE ( 'NONE', *, *, #120943, .F. ) ;
#39243=CARTESIAN_POINT ( 'NONE',  ( 34.92499999999998295, -11.99387692260791205, 4.000000000000000000 ) ) ;
#39244=DIRECTION ( 'NONE',  ( -0.7071067811865487940, 0.7071067811865463515, -0.000000000000000000 ) ) ;
#39245=ADVANCED_FACE ( 'NONE', ( #26421 ), #113407, .F. ) ;
#39246=DIRECTION ( 'NONE',  ( -0.7071067811865487940, 0.7071067811865463515, -0.000000000000000000 ) ) ;
#39248=DIRECTION ( 'NONE',  ( -0.7071067811865487940, 0.7071067811865463515, 0.000000000000000000 ) ) ;
#39250=PLANE ( 'NONE',  #79130 ) ;
#39252=ADVANCED_FACE ( 'NONE', ( #114813 ), #85071, .F. ) ;
#39255=ORIENTED_EDGE ( 'NONE', *, *, #29296, .T. ) ;
#39256=ORIENTED_EDGE ( 'NONE', *, *, #113630, .T. ) ;
#39257=VERTEX_POINT ( 'NONE', #30720 ) ;
#39259=ADVANCED_FACE ( 'NONE', ( #27837 ), #95228, .T. ) ;
#39260=VERTEX_POINT ( 'NONE', #16968 ) ;
#39261=ORIENTED_EDGE ( 'NONE', *, *, #75495, .F. ) ;
#39262=VERTEX_POINT ( 'NONE', #129276 ) ;
#39263=PLANE ( 'NONE',  #77974 ) ;
#39264=DIRECTION ( 'NONE',  ( -0.000000000000000000, 0.000000000000000000, 1.000000000000000000 ) ) ;
#39265=VERTEX_POINT ( 'NONE', #61923 ) ;
#39266=LINE ( 'NONE', #129104, #2225 ) ;
#39267=EDGE_CURVE ( 'NONE', #25758, #118900, #138758, .T. ) ;
#39269=CARTESIAN_POINT ( 'NONE',  ( 23.87852683662838871, -20.24070752338407075, 7.412974875817736731 ) ) ;
#39270=PLANE ( 'NONE',  #141386 ) ;
#39272=ORIENTED_EDGE ( 'NONE', *, *, #11729, .F. ) ;
#39273=CARTESIAN_POINT ( 'NONE',  ( -30.51665438641024153, 22.22500000000000142, 4.500000000000000888 ) ) ;
#39274=DIRECTION ( 'NONE',  ( -0.3543493200069162685, -0.000000000000000000, -0.9351131265310288487 ) ) ;
#39275=DIRECTION ( 'NONE',  ( -0.6830127018922181881, 0.6830127018922202975, -0.2588190451025214056 ) ) ;
#39278=FACE_OUTER_BOUND ( 'NONE', #47442, .T. ) ;
#39279=CARTESIAN_POINT ( 'NONE',  ( -5.510786437626906675, -27.52281430457051314, 5.000000000000000000 ) ) ;
#39281=LINE ( 'NONE', #15334, #25957 ) ;
#39282=DIRECTION ( 'NONE',  ( 0.7071067811865487940, -0.7071067811865463515, 0.000000000000000000 ) ) ;
#39283=ORIENTED_EDGE ( 'NONE', *, *, #119335, .F. ) ;
#39284=ORIENTED_EDGE ( 'NONE', *, *, #38489, .T. ) ;
#39286=ORIENTED_EDGE ( 'NONE', *, *, #101187, .T. ) ;
#39287=DIRECTION ( 'NONE',  ( -0.7071067811865487940, 0.7071067811865463515, 0.000000000000000000 ) ) ;
#39288=DIRECTION ( 'NONE',  ( 0.7071067811865487940, 0.7071067811865463515, 0.000000000000000000 ) ) ;
#39290=DIRECTION ( 'NONE',  ( 0.7071067811865487940, 0.7071067811865463515, 0.000000000000000000 ) ) ;
#39292=CARTESIAN_POINT ( 'NONE',  ( -28.82816939922333432, -20.24070752338407431, 4.000000000000000000 ) ) ;
#39293=EDGE_CURVE ( 'NONE', #100848, #133006, #94505, .T. ) ;
#39295=ORIENTED_EDGE ( 'NONE', *, *, #92167, .T. ) ;
#39296=EDGE_CURVE ( 'NONE', #35756, #104393, #139500, .T. ) ;
#39297=LINE ( 'NONE', #140044, #3961 ) ;
#39298=AXIS2_PLACEMENT_3D ( 'NONE', #62869, #83921, #16448 ) ;
#39299=ORIENTED_EDGE ( 'NONE', *, *, #5644, .F. ) ;
#39300=DIRECTION ( 'NONE',  ( -0.7071067811865486830, -0.7071067811865464625, 0.000000000000000000 ) ) ;
#39302=AXIS2_PLACEMENT_3D ( 'NONE', #9191, #120846, #141929 ) ;
#39303=VECTOR ( 'NONE', #35676, 1000.000000000000000 ) ;
#39304=CARTESIAN_POINT ( 'NONE',  ( 5.999999999999967137, -7.447814304570758104, 5.000000000000000000 ) ) ;
#39306=EDGE_CURVE ( 'NONE', #130956, #28809, #127891, .T. ) ;
#39307=VECTOR ( 'NONE', #127978, 1000.000000000000000 ) ;
#39311=ORIENTED_EDGE ( 'NONE', *, *, #83559, .F. ) ;
#39312=LINE ( 'NONE', #37892, #14640 ) ;
#39313=LINE ( 'NONE', #40047, #36928 ) ;
#39314=CARTESIAN_POINT ( 'NONE',  ( -25.49999999999982592, 16.77039438581777375, 0.4657186855308330098 ) ) ;
#39315=CARTESIAN_POINT ( 'NONE',  ( 29.67183060077626422, 17.25929247661553489, 4.000000000000000000 ) ) ;
#39316=VECTOR ( 'NONE', #23910, 1000.000000000000000 ) ;
#39317=AXIS2_PLACEMENT_3D ( 'NONE', #128543, #94462, #29210 ) ;
#39320=CARTESIAN_POINT ( 'NONE',  ( 5.999999999999956479, -6.108550654416955439, -3.114665004254954184 ) ) ;
#39321=EDGE_CURVE ( 'NONE', #19893, #77966, #87056, .T. ) ;
#39322=DIRECTION ( 'NONE',  ( 0.7071067811865486830, -0.7071067811865464625, -0.000000000000000000 ) ) ;
#39323=ORIENTED_EDGE ( 'NONE', *, *, #127314, .F. ) ;
#39324=VERTEX_POINT ( 'NONE', #138036 ) ;
#39325=VECTOR ( 'NONE', #112365, 1000.000000000000000 ) ;
#39327=DIRECTION ( 'NONE',  ( -0.000000000000000000, -0.3543493200069152693, 0.9351131265310292928 ) ) ;
#39329=VECTOR ( 'NONE', #62461, 1000.000000000000000 ) ;
#39330=FACE_OUTER_BOUND ( 'NONE', #42060, .T. ) ;
#39331=EDGE_CURVE ( 'NONE', #28081, #4087, #85781, .T. ) ;
#39336=CARTESIAN_POINT ( 'NONE',  ( -38.99451991528749062, 28.92564299267965211, 4.000000000000000000 ) ) ;
#39338=ADVANCED_FACE ( 'NONE', ( #96620 ), #95945, .F. ) ;
#39339=FACE_BOUND ( 'NONE', #109824, .T. ) ;
#39340=DIRECTION ( 'NONE',  ( -0.7071067811865486830, -0.7071067811865464625, 0.000000000000000000 ) ) ;
#39341=VECTOR ( 'NONE', #89959, 1000.000000000000000 ) ;
#39342=CARTESIAN_POINT ( 'NONE',  ( 22.00193056682082826, -22.22500000000000142, 4.500000000000000888 ) ) ;
#39343=CARTESIAN_POINT ( 'NONE',  ( -11.22995720542198406, 21.73644205237998150, 5.000000000000000888 ) ) ;
#39344=ORIENTED_EDGE ( 'NONE', *, *, #75603, .T. ) ;
#39346=CARTESIAN_POINT ( 'NONE',  ( 24.29974487139158867, -27.71228299555223273, 4.000000000000000000 ) ) ;
#39347=ORIENTED_EDGE ( 'NONE', *, *, #83180, .F. ) ;
#39348=VECTOR ( 'NONE', #96803, 1000.000000000000000 ) ;
#39349=ORIENTED_EDGE ( 'NONE', *, *, #64136, .F. ) ;
#39350=DIRECTION ( 'NONE',  ( 0.7071067811865487940, 0.7071067811865463515, 0.000000000000000000 ) ) ;
#39351=ORIENTED_EDGE ( 'NONE', *, *, #98881, .F. ) ;
#39352=ORIENTED_EDGE ( 'NONE', *, *, #65546, .T. ) ;
#39354=VERTEX_POINT ( 'NONE', #61241 ) ;
#39355=LINE ( 'NONE', #103839, #122817 ) ;
#39356=FACE_OUTER_BOUND ( 'NONE', #41834, .T. ) ;
#39357=ORIENTED_EDGE ( 'NONE', *, *, #21754, .T. ) ;
#39360=EDGE_CURVE ( 'NONE', #30958, #83476, #6748, .T. ) ;
#39361=ADVANCED_FACE ( 'NONE', ( #38722 ), #84392, .F. ) ;
#39363=LINE ( 'NONE', #37199, #82949 ) ;
#39364=CARTESIAN_POINT ( 'NONE',  ( 12.29974487139158512, -27.71228299555214747, 4.000000000000000000 ) ) ;
#39366=ORIENTED_EDGE ( 'NONE', *, *, #140215, .F. ) ;
#39367=VECTOR ( 'NONE', #42237, 1000.000000000000000 ) ;
#39368=ORIENTED_EDGE ( 'NONE', *, *, #80045, .F. ) ;
#39369=CARTESIAN_POINT ( 'NONE',  ( 69.48921356237309510, -27.52281430457103895, 5.000000000000000000 ) ) ;
#39370=CARTESIAN_POINT ( 'NONE',  ( -21.09843580608223945, 11.25929247661560595, 10.79108189686402142 ) ) ;
#39371=ORIENTED_EDGE ( 'NONE', *, *, #91007, .T. ) ;
#39372=ORIENTED_EDGE ( 'NONE', *, *, #107742, .F. ) ;
#39374=DIRECTION ( 'NONE',  ( -0.000000000000000000, -0.3543493200069152693, 0.9351131265310292928 ) ) ;
#39375=CARTESIAN_POINT ( 'NONE',  ( 26.99999999999981881, -22.06887692260759692, 4.000000000000000000 ) ) ;
#39377=PLANE ( 'NONE',  #57835 ) ;
#39378=ORIENTED_EDGE ( 'NONE', *, *, #45562, .F. ) ;
#39380=CARTESIAN_POINT ( 'NONE',  ( 2.671830600776456510, 5.259292476615662792, 4.000000000000000000 ) ) ;
#39383=ORIENTED_EDGE ( 'NONE', *, *, #132864, .F. ) ;
#39385=LINE ( 'NONE', #83614, #120585 ) ;
#39386=CARTESIAN_POINT ( 'NONE',  ( -30.48921356237309510, -27.52281430457076894, 5.000000000000000000 ) ) ;
#39387=ORIENTED_EDGE ( 'NONE', *, *, #121168, .T. ) ;
#39388=DIRECTION ( 'NONE',  ( -0.7071067811865486830, 0.7071067811865464625, 0.000000000000000000 ) ) ;
#39389=VERTEX_POINT ( 'NONE', #121963 ) ;
#39391=CARTESIAN_POINT ( 'NONE',  ( 18.18398860626898994, 28.73617430169800002, 5.000000000000000000 ) ) ;
#39392=CARTESIAN_POINT ( 'NONE',  ( 0.000000000000000000, 0.000000000000000000, 5.000000000000000000 ) ) ;
#39393=VERTEX_POINT ( 'NONE', #88665 ) ;
#39394=VECTOR ( 'NONE', #15094, 999.9999999999998863 ) ;
#39395=CARTESIAN_POINT ( 'NONE',  ( 41.99451991528749062, 28.92564299267967343, 4.000000000000000000 ) ) ;
#39396=CARTESIAN_POINT ( 'NONE',  ( 3.183988606268992161, 28.73617430169789699, 5.000000000000000000 ) ) ;
#39397=CARTESIAN_POINT ( 'NONE',  ( 24.48921356237309510, -27.52281430457072631, 5.000000000000000000 ) ) ;
#39398=EDGE_LOOP ( 'NONE', ( #72486, #1143, #33046, #57116 ) ) ;
#39399=VECTOR ( 'NONE', #118135, 1000.000000000000000 ) ;
#39400=VECTOR ( 'NONE', #15995, 1000.000000000000227 ) ;
#39403=PLANE ( 'NONE',  #26161 ) ;
#39404=LINE ( 'NONE', #83637, #7567 ) ;
#39406=PLANE ( 'NONE',  #42545 ) ;
#39408=EDGE_LOOP ( 'NONE', ( #114195, #123152, #106312, #49457 ) ) ;
#39409=VERTEX_POINT ( 'NONE', #895 ) ;
#39411=VECTOR ( 'NONE', #93973, 1000.000000000000000 ) ;
#39414=CARTESIAN_POINT ( 'NONE',  ( 48.48921356237309510, -27.52281430457089328, 5.000000000000000000 ) ) ;
#39415=ADVANCED_FACE ( 'NONE', ( #42312 ), #66899, .F. ) ;
#39416=DIRECTION ( 'NONE',  ( -0.7071067811865487940, 0.7071067811865463515, -0.000000000000000000 ) ) ;
#39417=CARTESIAN_POINT ( 'NONE',  ( 4.171830600776446296, 18.75929247661552779, 4.000000000000000000 ) ) ;
#39418=CARTESIAN_POINT ( 'NONE',  ( 17.81601139373099940, 28.73617430169775133, 5.000000000000000000 ) ) ;
#39419=ADVANCED_FACE ( 'NONE', ( #54606 ), #89359, .T. ) ;
#39421=FACE_OUTER_BOUND ( 'NONE', #24060, .T. ) ;
#39422=EDGE_CURVE ( 'NONE', #123534, #43910, #64757, .T. ) ;
#39423=DIRECTION ( 'NONE',  ( -0.7071067811865486830, -0.7071067811865464625, 0.000000000000000000 ) ) ;
#39424=CARTESIAN_POINT ( 'NONE',  ( 17.99451991528748351, 28.92564299267950645, 4.000000000000000000 ) ) ;
#39425=VECTOR ( 'NONE', #49230, 999.9999999999998863 ) ;
#39426=DIRECTION ( 'NONE',  ( 0.6830127018922180770, -0.6830127018922204085, -0.2588190451025213501 ) ) ;
#39431=AXIS2_PLACEMENT_3D ( 'NONE', #20713, #99706, #98300 ) ;
#39433=DIRECTION ( 'NONE',  ( 0.7071067811865487940, 0.7071067811865463515, 0.000000000000000000 ) ) ;
#39436=VECTOR ( 'NONE', #58384, 1000.000000000000000 ) ;
#39437=ORIENTED_EDGE ( 'NONE', *, *, #119407, .T. ) ;
#39438=DIRECTION ( 'NONE',  ( 0.7071067811865487940, 0.7071067811865463515, 0.000000000000000000 ) ) ;
#39440=CARTESIAN_POINT ( 'NONE',  ( -21.00548008471250938, 28.92564299267923644, 4.000000000000000000 ) ) ;
#39441=CARTESIAN_POINT ( 'NONE',  ( -22.49999999999984723, 15.05218569542901541, 5.000000000000000000 ) ) ;
#39443=FACE_OUTER_BOUND ( 'NONE', #21409, .T. ) ;
#39444=EDGE_CURVE ( 'NONE', #124629, #43828, #9630, .T. ) ;
#39445=CARTESIAN_POINT ( 'NONE',  ( -34.49999999999975131, -16.53574439159933718, 4.994342998332169437 ) ) ;
#39447=AXIS2_PLACEMENT_3D ( 'NONE', #39594, #62772, #106957 ) ;
#39448=VERTEX_POINT ( 'NONE', #21952 ) ;
#39449=LINE ( 'NONE', #18344, #46726 ) ;
#39450=LINE ( 'NONE', #106071, #139485 ) ;
#39451=DIRECTION ( 'NONE',  ( 0.3543493200069163240, 0.000000000000000000, 0.9351131265310288487 ) ) ;
#39452=CARTESIAN_POINT ( 'NONE',  ( -5.475998614145474619, 22.03583458319438293, 4.979811245910087614 ) ) ;
#39453=EDGE_CURVE ( 'NONE', #136490, #5707, #31419, .T. ) ;
#39456=CARTESIAN_POINT ( 'NONE',  ( -7.499999999999945821, -17.91344420646042934, 1.358650452708445311 ) ) ;
#39457=AXIS2_PLACEMENT_3D ( 'NONE', #54673, #1658, #34333 ) ;
#39458=ORIENTED_EDGE ( 'NONE', *, *, #25342, .T. ) ;
#39461=CARTESIAN_POINT ( 'NONE',  ( -5.671830600776434750, -9.740707523384186217, 4.000000000000000000 ) ) ;
#39462=FACE_OUTER_BOUND ( 'NONE', #17740, .T. ) ;
#39463=AXIS2_PLACEMENT_3D ( 'NONE', #1585, #132887, #64745 ) ;
#39464=EDGE_LOOP ( 'NONE', ( #110288, #97886, #106115, #6390 ) ) ;
#39465=PLANE ( 'NONE',  #23643 ) ;
#39466=CARTESIAN_POINT ( 'NONE',  ( 0.9891197134605101970, -22.02621442084247505, 4.990779571109222879 ) ) ;
#39470=ORIENTED_EDGE ( 'NONE', *, *, #77714, .T. ) ;
#39471=ORIENTED_EDGE ( 'NONE', *, *, #12952, .F. ) ;
#39472=VECTOR ( 'NONE', #131188, 1000.000000000000000 ) ;
#39473=CARTESIAN_POINT ( 'NONE',  ( 0.000000000000000000, 0.000000000000000000, 5.000000000000000000 ) ) ;
#39474=CARTESIAN_POINT ( 'NONE',  ( -25.49999999999982236, 1.466399257802255329, 5.000000000000000000 ) ) ;
#39475=PLANE ( 'NONE',  #7273 ) ;
#39477=DIRECTION ( 'NONE',  ( 0.7071067811865487940, 0.7071067811865463515, 0.000000000000000000 ) ) ;
#39479=ORIENTED_EDGE ( 'NONE', *, *, #22329, .T. ) ;
#39480=CARTESIAN_POINT ( 'NONE',  ( 16.49999999999988276, -15.29013452822853303, 0.3645803511610747893 ) ) ;
#39481=DIRECTION ( 'NONE',  ( -0.6830127018922180770, -0.6830127018922204085, -0.2588190451025213501 ) ) ;
#39482=LINE ( 'NONE', #49660, #28604 ) ;
#39483=CIRCLE ( 'NONE', #58030, 3.378199999999997871 ) ;
#39484=CARTESIAN_POINT ( 'NONE',  ( -32.99999999999977263, -0.2811185226894649669, -5.995736974527443586 ) ) ;
#39485=VECTOR ( 'NONE', #71858, 1000.000000000000227 ) ;
#39487=ORIENTED_EDGE ( 'NONE', *, *, #77044, .T. ) ;
#39488=FACE_OUTER_BOUND ( 'NONE', #71182, .T. ) ;
#39489=CARTESIAN_POINT ( 'NONE',  ( 54.18398860626899705, 28.73617430169825226, 5.000000000000000000 ) ) ;
#39490=LINE ( 'NONE', #28616, #135893 ) ;
#39491=ADVANCED_FACE ( 'NONE', ( #110369 ), #75640, .F. ) ;
#39492=CARTESIAN_POINT ( 'NONE',  ( 29.29298673570674438, -21.74070752338405654, 4.999753212805219782 ) ) ;
#39493=PLANE ( 'NONE',  #135851 ) ;
#39494=ORIENTED_EDGE ( 'NONE', *, *, #25417, .F. ) ;
#39495=ORIENTED_EDGE ( 'NONE', *, *, #19793, .F. ) ;
#39496=CARTESIAN_POINT ( 'NONE',  ( -8.999999999999937828, 2.966399257802232459, 5.000000000000000000 ) ) ;
#39498=AXIS2_PLACEMENT_3D ( 'NONE', #89264, #47760, #32024 ) ;
#39500=VECTOR ( 'NONE', #128310, 1000.000000000000114 ) ;
#39502=ORIENTED_EDGE ( 'NONE', *, *, #65172, .T. ) ;
#39504=CARTESIAN_POINT ( 'NONE',  ( 0.000000000000000000, 0.000000000000000000, 5.000000000000000000 ) ) ;
#39505=VERTEX_POINT ( 'NONE', #86521 ) ;
#39506=PLANE ( 'NONE',  #17848 ) ;
#39507=DIRECTION ( 'NONE',  ( -0.6830127018922181881, 0.6830127018922202975, -0.2588190451025214056 ) ) ;
#39508=AXIS2_PLACEMENT_3D ( 'NONE', #658, #44950, #89129 ) ;
#39509=AXIS2_PLACEMENT_3D ( 'NONE', #29416, #132350, #99665 ) ;
#39510=AXIS2_PLACEMENT_3D ( 'NONE', #41893, #98412, #8490 ) ;
#39511=VECTOR ( 'NONE', #111496, 1000.000000000000000 ) ;
#39513=EDGE_CURVE ( 'NONE', #138950, #131861, #87927, .T. ) ;
#39514=FACE_BOUND ( 'NONE', #22741, .T. ) ;
#39516=ADVANCED_FACE ( 'NONE', ( #55319 ), #98101, .F. ) ;
#39517=CARTESIAN_POINT ( 'NONE',  ( 30.48921356237309510, -27.52281430457076894, 5.000000000000000000 ) ) ;
#39518=AXIS2_PLACEMENT_3D ( 'NONE', #36243, #45711, #123969 ) ;
#39519=DIRECTION ( 'NONE',  ( 1.000000000000000000, 0.000000000000000000, 0.000000000000000000 ) ) ;
#39521=CARTESIAN_POINT ( 'NONE',  ( 24.18398860626899705, 28.73617430169804265, 5.000000000000000000 ) ) ;
#39522=VERTEX_POINT ( 'NONE', #78492 ) ;
#39523=ORIENTED_EDGE ( 'NONE', *, *, #41354, .T. ) ;
#39525=ORIENTED_EDGE ( 'NONE', *, *, #132217, .F. ) ;
#39527=VECTOR ( 'NONE', #130346, 1000.000000000000000 ) ;
#39528=CARTESIAN_POINT ( 'NONE',  ( 45.48921356237309510, -27.52281430457087197, 5.000000000000000000 ) ) ;
#39529=DIRECTION ( 'NONE',  ( 1.000000000000000000, 0.000000000000000000, 0.000000000000000000 ) ) ;
#39530=VECTOR ( 'NONE', #65186, 1000.000000000000000 ) ;
#39531=CARTESIAN_POINT ( 'NONE',  ( 45.29974487139158867, -27.71228299555237840, 4.000000000000000000 ) ) ;
#39532=ORIENTED_EDGE ( 'NONE', *, *, #87318, .T. ) ;
#39533=LINE ( 'NONE', #93177, #138640 ) ;
#39534=VECTOR ( 'NONE', #53042, 1000.000000000000000 ) ;
#39535=ADVANCED_FACE ( 'NONE', ( #164 ), #44461, .F. ) ;
#39536=DIRECTION ( 'NONE',  ( -0.7071067811865486830, -0.7071067811865464625, 0.000000000000000000 ) ) ;
#39537=VECTOR ( 'NONE', #46624, 1000.000000000000000 ) ;
#39538=CARTESIAN_POINT ( 'NONE',  ( -8.994519915287490619, 28.92564299267944250, 4.000000000000000000 ) ) ;
#39540=FACE_OUTER_BOUND ( 'NONE', #26104, .T. ) ;
#39541=ORIENTED_EDGE ( 'NONE', *, *, #130567, .F. ) ;
#39542=VECTOR ( 'NONE', #72966, 1000.000000000000000 ) ;
#39543=LINE ( 'NONE', #62011, #58896 ) ;
#39546=EDGE_CURVE ( 'NONE', #27314, #71394, #100243, .T. ) ;
#39547=ORIENTED_EDGE ( 'NONE', *, *, #37425, .T. ) ;
#39548=CIRCLE ( 'NONE', #127590, 5.968999999999998529 ) ;
#39549=EDGE_CURVE ( 'NONE', #16517, #19682, #135046, .T. ) ;
#39550=ORIENTED_EDGE ( 'NONE', *, *, #91855, .F. ) ;
#39552=ORIENTED_EDGE ( 'NONE', *, *, #14145, .T. ) ;
#39553=AXIS2_PLACEMENT_3D ( 'NONE', #40327, #142479, #128730 ) ;
#39557=CARTESIAN_POINT ( 'NONE',  ( -32.99999999999976552, -0.4125381241607533611, 4.000000000000000000 ) ) ;
#39558=ORIENTED_EDGE ( 'NONE', *, *, #81225, .T. ) ;
#39559=DIRECTION ( 'NONE',  ( -0.7071067811865487940, 0.7071067811865463515, -0.000000000000000000 ) ) ;
#39560=AXIS2_PLACEMENT_3D ( 'NONE', #1424, #101475, #36931 ) ;
#39561=FACE_OUTER_BOUND ( 'NONE', #116664, .T. ) ;
#39562=PLANE ( 'NONE',  #81863 ) ;
#39564=ORIENTED_EDGE ( 'NONE', *, *, #114012, .F. ) ;
#39565=EDGE_CURVE ( 'NONE', #16785, #55534, #69057, .T. ) ;
#39566=LINE ( 'NONE', #83796, #123315 ) ;
#39567=LINE ( 'NONE', #126536, #4379 ) ;
#39568=EDGE_LOOP ( 'NONE', ( #140537, #114922, #111367, #128076 ) ) ;
#39569=DIRECTION ( 'NONE',  ( 0.7071067811865487940, 0.7071067811865463515, 0.000000000000000000 ) ) ;
#39570=ORIENTED_EDGE ( 'NONE', *, *, #118922, .F. ) ;
#39572=ORIENTED_EDGE ( 'NONE', *, *, #64232, .T. ) ;
#39573=ORIENTED_EDGE ( 'NONE', *, *, #448, .F. ) ;
#39574=DIRECTION ( 'NONE',  ( -1.000000000000000000, 0.000000000000000000, 0.000000000000000000 ) ) ;
#39575=VECTOR ( 'NONE', #20815, 1000.000000000000000 ) ;
#39576=PLANE ( 'NONE',  #139513 ) ;
#39577=PLANE ( 'NONE',  #26281 ) ;
#39579=ORIENTED_EDGE ( 'NONE', *, *, #103395, .F. ) ;
#39580=CARTESIAN_POINT ( 'NONE',  ( -11.20710678118646442, -20.24070752338407431, 5.000000000000000000 ) ) ;
#39581=ORIENTED_EDGE ( 'NONE', *, *, #89660, .F. ) ;
#39582=AXIS2_PLACEMENT_3D ( 'NONE', #118391, #130739, #53131 ) ;
#39583=VECTOR ( 'NONE', #21737, 999.9999999999998863 ) ;
#39584=CARTESIAN_POINT ( 'NONE',  ( -32.99451991528749062, 28.92564299267960948, 4.000000000000000000 ) ) ;
#39586=DIRECTION ( 'NONE',  ( -0.7071067811865486830, 0.7071067811865464625, 0.000000000000000000 ) ) ;
#39588=LINE ( 'NONE', #106953, #55340 ) ;
#39590=ORIENTED_EDGE ( 'NONE', *, *, #132201, .F. ) ;
#39591=EDGE_CURVE ( 'NONE', #18615, #57817, #4414, .T. ) ;
#39593=VERTEX_POINT ( 'NONE', #113237 ) ;
#39594=CARTESIAN_POINT ( 'NONE',  ( -63.48921356237309510, -27.52281430457099631, 5.000000000000000000 ) ) ;
#39595=FACE_OUTER_BOUND ( 'NONE', #134069, .T. ) ;
#39596=DIRECTION ( 'NONE',  ( -0.7071067811865486830, -0.7071067811865464625, -0.000000000000000000 ) ) ;
#39597=LINE ( 'NONE', #130169, #31240 ) ;
#39598=AXIS2_PLACEMENT_3D ( 'NONE', #24572, #67397, #1368 ) ;
#39600=EDGE_CURVE ( 'NONE', #88422, #26808, #56781, .T. ) ;
#39602=ADVANCED_FACE ( 'NONE', ( #100940 ), #79958, .F. ) ;
#39604=AXIS2_PLACEMENT_3D ( 'NONE', #50409, #72199, #27930 ) ;
#39605=VECTOR ( 'NONE', #12191, 1000.000000000000000 ) ;
#39606=DIRECTION ( 'NONE',  ( -0.3543493200069162685, -0.000000000000000000, -0.9351131265310288487 ) ) ;
#39607=CARTESIAN_POINT ( 'NONE',  ( -24.48921356237309510, -27.52281430457072631, 5.000000000000000000 ) ) ;
#39608=DIRECTION ( 'NONE',  ( -0.7071067811865486830, -0.7071067811865464625, 0.000000000000000000 ) ) ;
#39609=SPHERICAL_SURFACE ( 'NONE', #99723, 0.5000000000000000000 ) ;
#39610=VERTEX_POINT ( 'NONE', #136422 ) ;
#39612=VECTOR ( 'NONE', #119274, 1000.000000000000000 ) ;
#39613=VECTOR ( 'NONE', #5126, 1000.000000000000114 ) ;
#39615=CARTESIAN_POINT ( 'NONE',  ( 33.18398860626899705, 28.73617430169810305, 5.000000000000000000 ) ) ;
#39616=ORIENTED_EDGE ( 'NONE', *, *, #33959, .F. ) ;
#39617=AXIS2_PLACEMENT_3D ( 'NONE', #26522, #114912, #25070 ) ;
#39618=DIRECTION ( 'NONE',  ( -0.000000000000000000, -0.3543493200069152693, 0.9351131265310292928 ) ) ;
#39619=CARTESIAN_POINT ( 'NONE',  ( 51.48921356237309510, -27.52281430457091460, 5.000000000000000000 ) ) ;
#39620=ORIENTED_EDGE ( 'NONE', *, *, #74954, .F. ) ;
#39623=DIRECTION ( 'NONE',  ( -0.6830127018922181881, 0.6830127018922202975, -0.2588190451025214056 ) ) ;
#39624=DIRECTION ( 'NONE',  ( -0.7071067811865486830, 0.7071067811865464625, 0.000000000000000000 ) ) ;
#39625=EDGE_LOOP ( 'NONE', ( #100922, #117835, #40707, #112912 ) ) ;
#39626=EDGE_LOOP ( 'NONE', ( #103296, #63483, #18204, #35650 ) ) ;
#39627=CARTESIAN_POINT ( 'NONE',  ( -11.70025512860841133, -27.71228299555198049, 4.000000000000000000 ) ) ;
#39631=ADVANCED_FACE ( 'NONE', ( #124129 ), #112538, .F. ) ;
#39633=CARTESIAN_POINT ( 'NONE',  ( 26.99999999999981171, 7.931123077392104648, 4.000000000000000000 ) ) ;
#39634=LINE ( 'NONE', #95406, #136271 ) ;
#39636=VECTOR ( 'NONE', #14170, 1000.000000000000000 ) ;
#39637=PLANE ( 'NONE',  #23811 ) ;
#39638=DIRECTION ( 'NONE',  ( -0.000000000000000000, -0.3543493200069152138, 0.9351131265310292928 ) ) ;
#39641=ADVANCED_FACE ( 'NONE', ( #36413 ), #13914, .F. ) ;
#39642=CARTESIAN_POINT ( 'NONE',  ( 28.49999999999980815, -16.53360074219757081, 5.000000000000000000 ) ) ;
#39643=ORIENTED_EDGE ( 'NONE', *, *, #56085, .T. ) ;
#39644=VECTOR ( 'NONE', #24161, 1000.000000000000227 ) ;
#39646=VERTEX_POINT ( 'NONE', #12500 ) ;
#39647=VECTOR ( 'NONE', #86548, 1000.000000000000000 ) ;
#39649=AXIS2_PLACEMENT_3D ( 'NONE', #29687, #118106, #18814 ) ;
#39650=CARTESIAN_POINT ( 'NONE',  ( -31.17183060077626067, -8.240707523384200428, 4.000000000000000000 ) ) ;
#39651=EDGE_CURVE ( 'NONE', #48429, #112121, #114661, .T. ) ;
#39653=PLANE ( 'NONE',  #38589 ) ;
#39654=VERTEX_POINT ( 'NONE', #58214 ) ;
#39656=PLANE ( 'NONE',  #74275 ) ;
#39657=DIRECTION ( 'NONE',  ( -0.7071067811865486830, -0.7071067811865464625, 0.000000000000000000 ) ) ;
#39658=LINE ( 'NONE', #139693, #119245 ) ;
#39659=EDGE_LOOP ( 'NONE', ( #38334, #130997, #125077, #82892 ) ) ;
#39660=ADVANCED_FACE ( 'NONE', ( #80643 ), #102405, .F. ) ;
#39661=DIRECTION ( 'NONE',  ( -0.7071067811865487940, 0.7071067811865463515, 0.000000000000000000 ) ) ;
#39662=DIRECTION ( 'NONE',  ( -0.000000000000000000, -0.3543493200069152693, 0.9351131265310292928 ) ) ;
#39664=VERTEX_POINT ( 'NONE', #25516 ) ;
#39665=EDGE_CURVE ( 'NONE', #54723, #128366, #101655, .T. ) ;
#39666=ORIENTED_EDGE ( 'NONE', *, *, #87568, .T. ) ;
#39668=EDGE_LOOP ( 'NONE', ( #68454, #84822, #51662, #3007 ) ) ;
#39669=CARTESIAN_POINT ( 'NONE',  ( 0.000000000000000000, -21.72500000000000142, 4.500000000000000888 ) ) ;
#39671=LINE ( 'NONE', #73027, #96594 ) ;
#39672=DIRECTION ( 'NONE',  ( 0.7071067811865487940, 0.7071067811865463515, 0.000000000000000000 ) ) ;
#39673=VERTEX_POINT ( 'NONE', #58935 ) ;
#39674=VECTOR ( 'NONE', #33198, 1000.000000000000000 ) ;
#39675=LINE ( 'NONE', #131666, #127929 ) ;
#39677=EDGE_LOOP ( 'NONE', ( #13093, #66036, #18850 ) ) ;
#39678=EDGE_CURVE ( 'NONE', #103755, #5851, #47346, .T. ) ;
#39679=DIRECTION ( 'NONE',  ( -0.000000000000000000, 0.3543493200069153248, 0.9351131265310292928 ) ) ;
#39681=DIRECTION ( 'NONE',  ( 0.7071067811865487940, 0.7071067811865463515, -0.000000000000000000 ) ) ;
#39682=CARTESIAN_POINT ( 'NONE',  ( -33.70710678118631165, 2.259292476615694323, 5.000000000000000000 ) ) ;
#39683=VECTOR ( 'NONE', #11169, 999.9999999999998863 ) ;
#39686=ADVANCED_FACE ( 'NONE', ( #37116 ), #81371, .F. ) ;
#39687=DIRECTION ( 'NONE',  ( -0.7071067811865486830, -0.7071067811865464625, 0.000000000000000000 ) ) ;
#39688=DIRECTION ( 'NONE',  ( 0.6830127018922180770, -0.6830127018922204085, -0.2588190451025213501 ) ) ;
#39689=DIRECTION ( 'NONE',  ( 0.3543493200069162685, -0.000000000000000000, -0.9351131265310288487 ) ) ;
#39690=CARTESIAN_POINT ( 'NONE',  ( -2.483345613589531542, 22.22500000000000142, 4.500000000000000888 ) ) ;
#39691=VECTOR ( 'NONE', #89883, 1000.000000000000000 ) ;
#39692=PLANE ( 'NONE',  #37262 ) ;
#39694=VERTEX_POINT ( 'NONE', #84230 ) ;
#39695=ORIENTED_EDGE ( 'NONE', *, *, #77882, .F. ) ;
#39697=ADVANCED_FACE ( 'NONE', ( #140025 ), #16794, .F. ) ;
#39698=AXIS2_PLACEMENT_3D ( 'NONE', #4018, #50455, #93229 ) ;
#39699=DIRECTION ( 'NONE',  ( 0.7071067811865487940, 0.7071067811865463515, 0.000000000000000000 ) ) ;
#39700=VECTOR ( 'NONE', #103857, 1000.000000000000000 ) ;
#39702=VERTEX_POINT ( 'NONE', #61072 ) ;
#39704=FACE_OUTER_BOUND ( 'NONE', #105960, .T. ) ;
#39705=EDGE_CURVE ( 'NONE', #140963, #98610, #50152, .T. ) ;
#39707=DIRECTION ( 'NONE',  ( -0.7071067811865487940, 0.7071067811865463515, 0.000000000000000000 ) ) ;
#39708=AXIS2_PLACEMENT_3D ( 'NONE', #129061, #56565, #45667 ) ;
#39709=VECTOR ( 'NONE', #68696, 1000.000000000000000 ) ;
#39710=AXIS2_PLACEMENT_3D ( 'NONE', #107150, #41921, #21589 ) ;
#39712=FACE_OUTER_BOUND ( 'NONE', #3253, .T. ) ;
#39713=ORIENTED_EDGE ( 'NONE', *, *, #105470, .F. ) ;
#39714=VECTOR ( 'NONE', #101039, 1000.000000000000000 ) ;
#39715=LINE ( 'NONE', #83943, #137392 ) ;
#39717=VERTEX_POINT ( 'NONE', #129119 ) ;
#39718=EDGE_CURVE ( 'NONE', #87654, #84329, #29101, .T. ) ;
#39719=FACE_OUTER_BOUND ( 'NONE', #25927, .T. ) ;
#39720=ORIENTED_EDGE ( 'NONE', *, *, #68388, .F. ) ;
#39721=CARTESIAN_POINT ( 'NONE',  ( -9.411614905948246346, 22.22500000000000142, 4.777194822843814137 ) ) ;
#39722=ADVANCED_FACE ( 'NONE', ( #8034 ), #16037, .F. ) ;
#39723=ORIENTED_EDGE ( 'NONE', *, *, #92350, .F. ) ;
#39724=EDGE_LOOP ( 'NONE', ( #75385, #8118, #57232, #88248 ) ) ;
#39725=VECTOR ( 'NONE', #138058, 1000.000000000000000 ) ;
#39728=CARTESIAN_POINT ( 'NONE',  ( -17.20666063542140378, 21.75929247661549937, 4.998822639870711626 ) ) ;
#39730=CARTESIAN_POINT ( 'NONE',  ( -71.99451991528749772, 28.92564299267988304, 4.000000000000000000 ) ) ;
#39732=VECTOR ( 'NONE', #101010, 1000.000000000000000 ) ;
#39733=FACE_OUTER_BOUND ( 'NONE', #76554, .T. ) ;
#39734=PLANE ( 'NONE',  #53349 ) ;
#39735=DIRECTION ( 'NONE',  ( 1.000000000000000000, 0.000000000000000000, 0.000000000000000000 ) ) ;
#39736=FACE_OUTER_BOUND ( 'NONE', #134461, .T. ) ;
#39737=ADVANCED_FACE ( 'NONE', ( #115350 ), #5883, .F. ) ;
#39738=AXIS2_PLACEMENT_3D ( 'NONE', #92077, #125448, #137029 ) ;
#39739=DIRECTION ( 'NONE',  ( 0.7071067811865487940, 0.7071067811865463515, -0.000000000000000000 ) ) ;
#39740=VERTEX_POINT ( 'NONE', #128426 ) ;
#39741=VECTOR ( 'NONE', #10042, 1000.000000000000000 ) ;
#39742=CARTESIAN_POINT ( 'NONE',  ( 33.18398860626899705, 28.73617430169810305, 5.000000000000000000 ) ) ;
#39743=LINE ( 'NONE', #49190, #91482 ) ;
#39745=AXIS2_PLACEMENT_3D ( 'NONE', #18275, #62551, #106725 ) ;
#39746=ORIENTED_EDGE ( 'NONE', *, *, #73880, .T. ) ;
#39748=ADVANCED_FACE ( 'NONE', ( #18183 ), #73339, .F. ) ;
#39749=ORIENTED_EDGE ( 'NONE', *, *, #4315, .T. ) ;
#39751=DIRECTION ( 'NONE',  ( 0.7071067811865487940, 0.7071067811865463515, -0.000000000000000000 ) ) ;
#39752=CARTESIAN_POINT ( 'NONE',  ( -28.96836484077790885, 2.259292476615697876, 13.77329220150630462 ) ) ;
#39753=VECTOR ( 'NONE', #136221, 1000.000000000000000 ) ;
#39755=DIRECTION ( 'NONE',  ( -0.7071067811865487940, 0.7071067811865463515, 0.000000000000000000 ) ) ;
#39756=ORIENTED_EDGE ( 'NONE', *, *, #86468, .T. ) ;
#39757=ORIENTED_EDGE ( 'NONE', *, *, #26455, .F. ) ;
#39760=LINE ( 'NONE', #39019, #49002 ) ;
#39761=CYLINDRICAL_SURFACE ( 'NONE', #103723, 0.5000000000000004441 ) ;
#39762=CARTESIAN_POINT ( 'NONE',  ( 32.67183060077624646, 20.25929247661551003, 4.000000000000000000 ) ) ;
#39763=VERTEX_POINT ( 'NONE', #26950 ) ;
#39764=EDGE_CURVE ( 'NONE', #129163, #119037, #105917, .T. ) ;
#39765=EDGE_LOOP ( 'NONE', ( #123810, #98735, #16989, #28083 ) ) ;
#39766=VECTOR ( 'NONE', #80492, 1000.000000000000000 ) ;
#39767=ORIENTED_EDGE ( 'NONE', *, *, #24609, .F. ) ;
#39769=PLANE ( 'NONE',  #64967 ) ;
#39770=CARTESIAN_POINT ( 'NONE',  ( -1.499999999999987566, -8.947814304570737676, 5.000000000000000000 ) ) ;
#39771=AXIS2_PLACEMENT_3D ( 'NONE', #25480, #11017, #33556 ) ;
#39772=DIRECTION ( 'NONE',  ( 0.7071067811865487940, -0.7071067811865463515, 0.000000000000000000 ) ) ;
#39773=CARTESIAN_POINT ( 'NONE',  ( -36.48921356237310221, -27.52281430457080802, 5.000000000000000000 ) ) ;
#39774=ADVANCED_FACE ( 'NONE', ( #38554 ), #82781, .F. ) ;
#39775=EDGE_CURVE ( 'NONE', #118193, #99040, #118955, .T. ) ;
#39776=CARTESIAN_POINT ( 'NONE',  ( -34.49999999999976552, -9.462702396501047275, -9.474982329943436810 ) ) ;
#39777=DIRECTION ( 'NONE',  ( -0.6830127018922180770, -0.6830127018922204085, -0.2588190451025213501 ) ) ;
#39778=LINE ( 'NONE', #40488, #72233 ) ;
#39779=CARTESIAN_POINT ( 'NONE',  ( 33.48921356237309510, -27.52281430457078670, 5.000000000000000000 ) ) ;
#39780=AXIS2_PLACEMENT_3D ( 'NONE', #115794, #27377, #74501 ) ;
#39781=ORIENTED_EDGE ( 'NONE', *, *, #75441, .T. ) ;
#39782=LINE ( 'NONE', #71678, #55666 ) ;
#39783=VECTOR ( 'NONE', #31367, 1000.000000000000000 ) ;
#39784=DIRECTION ( 'NONE',  ( 0.7071067811865487940, 0.7071067811865463515, 0.000000000000000000 ) ) ;
#39787=LINE ( 'NONE', #95555, #11237 ) ;
#39789=ORIENTED_EDGE ( 'NONE', *, *, #70095, .T. ) ;
#39790=EDGE_CURVE ( 'NONE', #12370, #34226, #44286, .T. ) ;
#39791=ADVANCED_FACE ( 'NONE', ( #64586 ), #119642, .F. ) ;
#39792=PLANE ( 'NONE',  #42281 ) ;
#39793=LINE ( 'NONE', #50637, #71600 ) ;
#39795=ORIENTED_EDGE ( 'NONE', *, *, #131111, .F. ) ;
#39797=VERTEX_POINT ( 'NONE', #66733 ) ;
#39798=LINE ( 'NONE', #38346, #91559 ) ;
#39801=DIRECTION ( 'NONE',  ( 1.000000000000000000, 0.000000000000000000, 0.000000000000000000 ) ) ;
#39803=DIRECTION ( 'NONE',  ( 0.7071067811865486830, -0.7071067811865464625, -0.000000000000000000 ) ) ;
#39804=DIRECTION ( 'NONE',  ( 0.3543493200069162685, -0.000000000000000000, -0.9351131265310288487 ) ) ;
#39809=LINE ( 'NONE', #16575, #13518 ) ;
#39810=VECTOR ( 'NONE', #48865, 1000.000000000000000 ) ;
#39811=EDGE_CURVE ( 'NONE', #128354, #132699, #33426, .T. ) ;
#39812=VECTOR ( 'NONE', #89289, 1000.000000000000114 ) ;
#39813=CARTESIAN_POINT ( 'NONE',  ( -24.29974487139158867, -27.71228299555223273, 4.000000000000000000 ) ) ;
#39814=CARTESIAN_POINT ( 'NONE',  ( -5.994519915287488843, 28.92564299267942118, 4.000000000000000000 ) ) ;
#39815=ORIENTED_EDGE ( 'NONE', *, *, #87487, .T. ) ;
#39817=VECTOR ( 'NONE', #57048, 999.9999999999998863 ) ;
#39819=VECTOR ( 'NONE', #132787, 1000.000000000000000 ) ;
#39820=DIRECTION ( 'NONE',  ( -0.7071067811865486830, -0.7071067811865464625, -0.000000000000000000 ) ) ;
#39821=VERTEX_POINT ( 'NONE', #42144 ) ;
#39823=LINE ( 'NONE', #39076, #41791 ) ;
#39824=AXIS2_PLACEMENT_3D ( 'NONE', #81728, #136779, #125924 ) ;
#39827=FACE_OUTER_BOUND ( 'NONE', #81750, .T. ) ;
#39828=ORIENTED_EDGE ( 'NONE', *, *, #69861, .T. ) ;
#39829=CARTESIAN_POINT ( 'NONE',  ( -9.489213562373095101, -27.52281430457062328, 5.000000000000000000 ) ) ;
#39831=CARTESIAN_POINT ( 'NONE',  ( 29.58838509405148542, 22.22500000000000142, 4.777194822843815913 ) ) ;
#39833=DIRECTION ( 'NONE',  ( 1.000000000000000000, 0.000000000000000000, 0.000000000000000000 ) ) ;
#39834=DIRECTION ( 'NONE',  ( -0.000000000000000000, 0.000000000000000000, 1.000000000000000000 ) ) ;
#39835=EDGE_CURVE ( 'NONE', #139444, #42123, #88498, .T. ) ;
#39836=DIRECTION ( 'NONE',  ( -0.6830127018922181881, 0.6830127018922202975, -0.2588190451025214056 ) ) ;
#39837=PLANE ( 'NONE',  #111792 ) ;
#39838=PLANE ( 'NONE',  #107888 ) ;
#39841=EDGE_CURVE ( 'NONE', #118711, #125243, #142169, .T. ) ;
#39842=ORIENTED_EDGE ( 'NONE', *, *, #74287, .F. ) ;
#39843=ORIENTED_EDGE ( 'NONE', *, *, #94807, .T. ) ;
#39845=ORIENTED_EDGE ( 'NONE', *, *, #107708, .F. ) ;
#39846=DIRECTION ( 'NONE',  ( -0.7071067811865486830, 0.7071067811865464625, 0.000000000000000000 ) ) ;
#39847=ORIENTED_EDGE ( 'NONE', *, *, #7110, .T. ) ;
#39848=EDGE_CURVE ( 'NONE', #8196, #42180, #729, .T. ) ;
#39849=CARTESIAN_POINT ( 'NONE',  ( 29.20710678118634007, 9.759292476615620160, 5.000000000000000000 ) ) ;
#39850=PLANE ( 'NONE',  #95143 ) ;
#39851=VECTOR ( 'NONE', #87482, 999.9999999999998863 ) ;
#39854=ORIENTED_EDGE ( 'NONE', *, *, #23546, .F. ) ;
#39855=VECTOR ( 'NONE', #120263, 1000.000000000000227 ) ;
#39856=CARTESIAN_POINT ( 'NONE',  ( -22.82816939922336630, 18.75929247661553845, 4.000000000000000000 ) ) ;
#39858=CARTESIAN_POINT ( 'NONE',  ( 23.55512991947088963, -0.7407075233842735917, 4.307968247157003994 ) ) ;
#39859=LINE ( 'NONE', #29640, #35656 ) ;
#39860=VECTOR ( 'NONE', #14660, 1000.000000000000000 ) ;
#39861=DIRECTION ( 'NONE',  ( -0.000000000000000000, -0.3543493200069152693, 0.9351131265310292928 ) ) ;
#39862=ORIENTED_EDGE ( 'NONE', *, *, #140064, .F. ) ;
#39863=VERTEX_POINT ( 'NONE', #55148 ) ;
#39864=ORIENTED_EDGE ( 'NONE', *, *, #58949, .T. ) ;
#39865=CARTESIAN_POINT ( 'NONE',  ( -12.48921356237309155, -27.52281430457064104, 5.000000000000000000 ) ) ;
#39866=CARTESIAN_POINT ( 'NONE',  ( -29.99999999999978684, 8.966399257802176948, 5.000000000000000000 ) ) ;
#39868=AXIS2_PLACEMENT_3D ( 'NONE', #42212, #74111, #73408 ) ;
#39870=ORIENTED_EDGE ( 'NONE', *, *, #1166, .T. ) ;
#39871=ORIENTED_EDGE ( 'NONE', *, *, #56991, .T. ) ;
#39872=LINE ( 'NONE', #50022, #27082 ) ;
#39873=VERTEX_POINT ( 'NONE', #87054 ) ;
#39874=EDGE_CURVE ( 'NONE', #140745, #108674, #131999, .T. ) ;
#39875=VERTEX_POINT ( 'NONE', #99326 ) ;
#39877=VECTOR ( 'NONE', #113034, 1000.000000000000000 ) ;
#39879=CARTESIAN_POINT ( 'NONE',  ( -3.489213562373097322, -27.52281430457057709, 5.000000000000000000 ) ) ;
#39880=CARTESIAN_POINT ( 'NONE',  ( -30.70612307739174796, 22.22500000000000142, 4.000000000000000000 ) ) ;
#39881=ORIENTED_EDGE ( 'NONE', *, *, #129354, .F. ) ;
#39882=LINE ( 'NONE', #139902, #43733 ) ;
#39883=FACE_OUTER_BOUND ( 'NONE', #138925, .T. ) ;
#39884=VECTOR ( 'NONE', #72606, 1000.000000000000000 ) ;
#39885=DIRECTION ( 'NONE',  ( -0.7071067811865486830, -0.7071067811865464625, -0.000000000000000000 ) ) ;
#39886=( BOUNDED_CURVE ( )  B_SPLINE_CURVE ( 3, ( #63665, #141180, #140471, #62952 ),
 .UNSPECIFIED., .F., .T. ) 
 B_SPLINE_CURVE_WITH_KNOTS ( ( 4, 4 ),
 ( 2.001653308786179419, 3.503810798801449522 ),
 .UNSPECIFIED. ) 
 CURVE ( )  GEOMETRIC_REPRESENTATION_ITEM ( )  RATIONAL_B_SPLINE_CURVE ( ( 1.000000000000000000, 0.8206354192515267210, 0.8206354192515267210, 1.000000000000000000 ) ) 
 REPRESENTATION_ITEM ( '' )  );
#39887=CARTESIAN_POINT ( 'NONE',  ( 25.49999999999982236, 3.073033219394647464, -6.593910359670911880 ) ) ;
#39888=ORIENTED_EDGE ( 'NONE', *, *, #95403, .F. ) ;
#39889=EDGE_CURVE ( 'NONE', #82163, #114199, #63889, .T. ) ;
#39890=DIRECTION ( 'NONE',  ( 0.6830127018922180770, -0.6830127018922204085, -0.2588190451025213501 ) ) ;
#39891=ORIENTED_EDGE ( 'NONE', *, *, #20453, .F. ) ;
#39893=EDGE_CURVE ( 'NONE', #12168, #132912, #86355, .T. ) ;
#39894=DIRECTION ( 'NONE',  ( -0.000000000000000000, 0.3543493200069153248, 0.9351131265310292928 ) ) ;
#39895=ORIENTED_EDGE ( 'NONE', *, *, #20664, .F. ) ;
#39896=DIRECTION ( 'NONE',  ( -0.7071067811865486830, -0.7071067811865464625, 0.000000000000000000 ) ) ;
#39897=ORIENTED_EDGE ( 'NONE', *, *, #138664, .F. ) ;
#39898=EDGE_LOOP ( 'NONE', ( #2600, #25369, #130385, #52918 ) ) ;
#39899=ORIENTED_EDGE ( 'NONE', *, *, #14896, .F. ) ;
#39900=ADVANCED_FACE ( 'NONE', ( #130574 ), #98627, .F. ) ;
#39901=EDGE_CURVE ( 'NONE', #88238, #69036, #61057, .T. ) ;
#39903=LINE ( 'NONE', #125464, #85356 ) ;
#39904=DIRECTION ( 'NONE',  ( 0.7071067811865487940, 0.7071067811865463515, 0.000000000000000000 ) ) ;
#39906=FACE_OUTER_BOUND ( 'NONE', #22540, .T. ) ;
#39907=EDGE_CURVE ( 'NONE', #93479, #74127, #76039, .T. ) ;
#39908=DIRECTION ( 'NONE',  ( 0.7071067811865487940, -0.7071067811865463515, 0.000000000000000000 ) ) ;
#39909=VECTOR ( 'NONE', #8507, 1000.000000000000000 ) ;
#39910=AXIS2_PLACEMENT_3D ( 'NONE', #56894, #44601, #109807 ) ;
#39912=DIRECTION ( 'NONE',  ( -0.7071067811865487940, 0.7071067811865463515, -0.000000000000000000 ) ) ;
#39913=VECTOR ( 'NONE', #47451, 1000.000000000000000 ) ;
#39914=EDGE_CURVE ( 'NONE', #10965, #95953, #13034, .T. ) ;
#39915=AXIS2_PLACEMENT_3D ( 'NONE', #44161, #98521, #22357 ) ;
#39916=CARTESIAN_POINT ( 'NONE',  ( 62.99451991528749772, 28.92564299267982264, 4.000000000000000000 ) ) ;
#39917=LINE ( 'NONE', #51487, #85322 ) ;
#39918=FACE_OUTER_BOUND ( 'NONE', #40499, .T. ) ;
#39919=ORIENTED_EDGE ( 'NONE', *, *, #59219, .F. ) ;
#39920=VERTEX_POINT ( 'NONE', #91361 ) ;
#39921=VECTOR ( 'NONE', #52985, 1000.000000000000227 ) ;
#39922=ORIENTED_EDGE ( 'NONE', *, *, #136413, .F. ) ;
#39923=VECTOR ( 'NONE', #93803, 999.9999999999998863 ) ;
#39924=ORIENTED_EDGE ( 'NONE', *, *, #123082, .F. ) ;
#39928=ORIENTED_EDGE ( 'NONE', *, *, #9473, .T. ) ;
#39929=EDGE_LOOP ( 'NONE', ( #94900, #135109, #20254, #11540 ) ) ;
#39931=CARTESIAN_POINT ( 'NONE',  ( 27.29974487139158512, -27.71228299555225405, 4.000000000000000000 ) ) ;
#39932=PLANE ( 'NONE',  #111171 ) ;
#39933=ORIENTED_EDGE ( 'NONE', *, *, #124525, .T. ) ;
#39934=PLANE ( 'NONE',  #120428 ) ;
#39935=EDGE_CURVE ( 'NONE', #115217, #131076, #100783, .T. ) ;
#39936=EDGE_CURVE ( 'NONE', #25329, #903, #134874, .T. ) ;
#39937=ORIENTED_EDGE ( 'NONE', *, *, #18143, .T. ) ;
#39938=CARTESIAN_POINT ( 'NONE',  ( -29.99999999999979039, 8.587461875839160541, 4.000000000000000000 ) ) ;
#39939=FACE_OUTER_BOUND ( 'NONE', #122108, .T. ) ;
#39941=ORIENTED_EDGE ( 'NONE', *, *, #135904, .F. ) ;
#39944=LINE ( 'NONE', #128362, #41967 ) ;
#39946=EDGE_CURVE ( 'NONE', #130142, #27289, #124673, .T. ) ;
#39947=ORIENTED_EDGE ( 'NONE', *, *, #1846, .T. ) ;
#39948=DIRECTION ( 'NONE',  ( 0.7071067811865487940, -0.7071067811865463515, 0.000000000000000000 ) ) ;
#39949=ORIENTED_EDGE ( 'NONE', *, *, #123821, .T. ) ;
#39950=DIRECTION ( 'NONE',  ( 0.3543493200069164351, 2.781805975412904658E-17, -0.9351131265310288487 ) ) ;
#39951=CARTESIAN_POINT ( 'NONE',  ( 45.48921356237309510, -27.52281430457087197, 5.000000000000000000 ) ) ;
#39952=DIRECTION ( 'NONE',  ( -0.7071067811865486830, 0.7071067811865464625, 0.000000000000000000 ) ) ;
#39954=VERTEX_POINT ( 'NONE', #89893 ) ;
#39955=VECTOR ( 'NONE', #69688, 1000.000000000000000 ) ;
#39956=EDGE_CURVE ( 'NONE', #105156, #138063, #23188, .T. ) ;
#39958=CARTESIAN_POINT ( 'NONE',  ( -20.81601139373100295, 28.73617430169773002, 5.000000000000000000 ) ) ;
#39959=AXIS2_PLACEMENT_3D ( 'NONE', #95515, #139778, #50601 ) ;
#39960=CARTESIAN_POINT ( 'NONE',  ( 45.18398860626900415, 28.73617430169818832, 5.000000000000000000 ) ) ;
#39961=DIRECTION ( 'NONE',  ( 0.3543493200069163240, -0.000000000000000000, -0.9351131265310288487 ) ) ;
#39962=ORIENTED_EDGE ( 'NONE', *, *, #140418, .F. ) ;
#39963=DIRECTION ( 'NONE',  ( -0.7071067811865487940, 0.7071067811865463515, -0.000000000000000000 ) ) ;
#39964=AXIS2_PLACEMENT_3D ( 'NONE', #25354, #113800, #135571 ) ;
#39965=DIRECTION ( 'NONE',  ( -0.7071067811865487940, 0.7071067811865463515, 0.000000000000000000 ) ) ;
#39966=EDGE_CURVE ( 'NONE', #41713, #114574, #14486, .T. ) ;
#39967=ORIENTED_EDGE ( 'NONE', *, *, #107470, .F. ) ;
#39969=ORIENTED_EDGE ( 'NONE', *, *, #4762, .T. ) ;
#39970=ADVANCED_FACE ( 'NONE', ( #23947 ), #68205, .F. ) ;
#39971=EDGE_LOOP ( 'NONE', ( #42779, #102472, #102848, #12287, #121317, #79871 ) ) ;
#39973=EDGE_LOOP ( 'NONE', ( #87124, #89081, #58825, #13653 ) ) ;
#39975=CARTESIAN_POINT ( 'NONE',  ( -44.99451991528749772, 28.92564299267969474, 4.000000000000000000 ) ) ;
#39976=LINE ( 'NONE', #84195, #22904 ) ;
#39978=DIRECTION ( 'NONE',  ( -0.6830127018922180770, -0.6830127018922204085, -0.2588190451025213501 ) ) ;
#39980=DIRECTION ( 'NONE',  ( -0.6830127018922180770, -0.6830127018922204085, -0.2588190451025213501 ) ) ;
#39981=VECTOR ( 'NONE', #8238, 1000.000000000000000 ) ;
#39982=DIRECTION ( 'NONE',  ( -0.7071067811865486830, -0.7071067811865464625, 0.000000000000000000 ) ) ;
#39983=CARTESIAN_POINT ( 'NONE',  ( -13.82816939922343735, -5.240707523384227073, 4.000000000000000000 ) ) ;
#39984=CARTESIAN_POINT ( 'NONE',  ( -23.18753812416036908, -22.22500000000000142, 4.000000000000000000 ) ) ;
#39985=AXIS2_PLACEMENT_3D ( 'NONE', #46971, #140347, #118587 ) ;
#39986=CARTESIAN_POINT ( 'NONE',  ( 21.05633424050521540, 8.797022467481218300, 4.404357971607193889 ) ) ;
#39987=EDGE_CURVE ( 'NONE', #28420, #41423, #92032, .T. ) ;
#39988=CARTESIAN_POINT ( 'NONE',  ( -19.49999999999986500, -16.53360074219757081, 5.000000000000000000 ) ) ;
#39989=LINE ( 'NONE', #5861, #131114 ) ;
#39990=ORIENTED_EDGE ( 'NONE', *, *, #77589, .F. ) ;
#39991=ORIENTED_EDGE ( 'NONE', *, *, #19378, .F. ) ;
#39992=EDGE_LOOP ( 'NONE', ( #23707, #105995, #97748, #106026, #30442 ) ) ;
#39994=ORIENTED_EDGE ( 'NONE', *, *, #126790, .F. ) ;
#39995=VERTEX_POINT ( 'NONE', #1436 ) ;
#39996=VERTEX_POINT ( 'NONE', #112380 ) ;
#39997=DIRECTION ( 'NONE',  ( 1.000000000000000000, 0.000000000000000000, 0.000000000000000000 ) ) ;
#39998=LINE ( 'NONE', #27643, #25410 ) ;
#39999=VECTOR ( 'NONE', #131673, 1000.000000000000227 ) ;
#40000=EDGE_LOOP ( 'NONE', ( #52181, #78757, #62103, #2431 ) ) ;
#40001=CARTESIAN_POINT ( 'NONE',  ( 21.29974487139158512, -27.71228299555221142, 4.000000000000000000 ) ) ;
#40002=DIRECTION ( 'NONE',  ( 0.3543493200069162685, -0.000000000000000000, -0.9351131265310288487 ) ) ;
#40003=LINE ( 'NONE', #29092, #11623 ) ;
#40004=CARTESIAN_POINT ( 'NONE',  ( 33.48921356237309510, -27.52281430457078670, 5.000000000000000000 ) ) ;
#40007=CARTESIAN_POINT ( 'NONE',  ( -30.79333936457826226, 21.75929247661549581, 4.998822639870701856 ) ) ;
#40009=CARTESIAN_POINT ( 'NONE',  ( -25.49999999999982236, 8.900465351122130997, -2.516491619111453915 ) ) ;
#40010=VECTOR ( 'NONE', #13913, 1000.000000000000000 ) ;
#40011=CARTESIAN_POINT ( 'NONE',  ( 30.18398860626900060, 28.73617430169808173, 5.000000000000000000 ) ) ;
#40012=CARTESIAN_POINT ( 'NONE',  ( -51.18398860626899705, 28.73617430169823095, 5.000000000000000000 ) ) ;
#40013=DIRECTION ( 'NONE',  ( 0.7071067811865487940, 0.7071067811865463515, 0.000000000000000000 ) ) ;
#40014=DIRECTION ( 'NONE',  ( -0.6830127018922181881, 0.6830127018922202975, -0.2588190451025214056 ) ) ;
#40016=CARTESIAN_POINT ( 'NONE',  ( -19.49999999999985789, 19.08746187583904330, 4.000000000000000000 ) ) ;
#40017=ADVANCED_FACE ( 'NONE', ( #57311 ), #36941, .F. ) ;
#40018=DIRECTION ( 'NONE',  ( 0.7071067811865487940, 0.7071067811865463515, -0.000000000000000000 ) ) ;
#40019=VERTEX_POINT ( 'NONE', #2883 ) ;
#40020=ORIENTED_EDGE ( 'NONE', *, *, #141728, .F. ) ;
#40022=ORIENTED_EDGE ( 'NONE', *, *, #66125, .T. ) ;
#40023=CARTESIAN_POINT ( 'NONE',  ( -23.54739889332687497, 7.099584588756134629, 5.000000000000000000 ) ) ;
#40024=DIRECTION ( 'NONE',  ( -0.7071067811865487940, 0.7071067811865463515, -0.000000000000000000 ) ) ;
#40025=VECTOR ( 'NONE', #4544, 1000.000000000000114 ) ;
#40026=AXIS2_PLACEMENT_3D ( 'NONE', #22320, #123839, #99924 ) ;
#40027=DIRECTION ( 'NONE',  ( 0.7071067811865486830, -0.7071067811865464625, -0.000000000000000000 ) ) ;
#40028=DIRECTION ( 'NONE',  ( -0.6830127018922181881, 0.6830127018922202975, -0.2588190451025214056 ) ) ;
#40029=VECTOR ( 'NONE', #72042, 999.9999999999998863 ) ;
#40030=DIRECTION ( 'NONE',  ( 0.7071067811865487940, -0.7071067811865463515, 0.000000000000000000 ) ) ;
#40031=LINE ( 'NONE', #53746, #11717 ) ;
#40034=ORIENTED_EDGE ( 'NONE', *, *, #100272, .F. ) ;
#40035=DIRECTION ( 'NONE',  ( -0.7071067811865486830, -0.7071067811865464625, 0.000000000000000000 ) ) ;
#40036=ORIENTED_EDGE ( 'NONE', *, *, #71154, .T. ) ;
#40038=VECTOR ( 'NONE', #11398, 1000.000000000000000 ) ;
#40039=LINE ( 'NONE', #28422, #114609 ) ;
#40042=DIRECTION ( 'NONE',  ( -0.3543493200069162685, -0.000000000000000000, -0.9351131265310288487 ) ) ;
#40045=ORIENTED_EDGE ( 'NONE', *, *, #115392, .F. ) ;
#40046=DIRECTION ( 'NONE',  ( 0.7071067811865486830, -0.7071067811865464625, -0.000000000000000000 ) ) ;
#40047=CARTESIAN_POINT ( 'NONE',  ( 38.99451991528749062, 28.92564299267965211, 4.000000000000000000 ) ) ;
#40048=DIRECTION ( 'NONE',  ( 0.7071067811865486830, -0.7071067811865464625, -0.000000000000000000 ) ) ;
#40049=LINE ( 'NONE', #74814, #30160 ) ;
#40053=LINE ( 'NONE', #78187, #25705 ) ;
#40054=CARTESIAN_POINT ( 'NONE',  ( 29.29289321881325137, 8.259292476615643253, 5.000000000000000000 ) ) ;
#40057=EDGE_LOOP ( 'NONE', ( #63715, #123263, #50351, #105434 ) ) ;
#40058=AXIS2_PLACEMENT_3D ( 'NONE', #60054, #134777, #137611 ) ;
#40062=VECTOR ( 'NONE', #62754, 1000.000000000000000 ) ;
#40064=VECTOR ( 'NONE', #75152, 1000.000000000000227 ) ;
#40066=EDGE_CURVE ( 'NONE', #64057, #38139, #111665, .T. ) ;
#40067=FACE_BOUND ( 'NONE', #45462, .T. ) ;
#40069=EDGE_CURVE ( 'NONE', #117114, #25784, #101485, .T. ) ;
#40070=EDGE_CURVE ( 'NONE', #88880, #10438, #113070, .T. ) ;
#40071=PLANE ( 'NONE',  #12030 ) ;
#40072=ORIENTED_EDGE ( 'NONE', *, *, #110419, .F. ) ;
#40073=DIRECTION ( 'NONE',  ( 0.3543493200069162685, -0.000000000000000000, -0.9351131265310288487 ) ) ;
#40074=DIRECTION ( 'NONE',  ( -0.7071067811865486830, -0.7071067811865464625, 0.000000000000000000 ) ) ;
#40075=EDGE_LOOP ( 'NONE', ( #53009, #122620, #31245, #59809 ) ) ;
#40076=VERTEX_POINT ( 'NONE', #47179 ) ;
#40077=LINE ( 'NONE', #51646, #125909 ) ;
#40078=ORIENTED_EDGE ( 'NONE', *, *, #122793, .F. ) ;
#40079=VECTOR ( 'NONE', #66693, 1000.000000000000000 ) ;
#40080=EDGE_CURVE ( 'NONE', #97623, #62679, #29619, .T. ) ;
#40081=ADVANCED_FACE ( 'NONE', ( #116644 ), #39838, .F. ) ;
#40083=ORIENTED_EDGE ( 'NONE', *, *, #82077, .F. ) ;
#40084=CARTESIAN_POINT ( 'NONE',  ( -15.18398860626900237, 28.73617430169797871, 5.000000000000000000 ) ) ;
#40085=LINE ( 'NONE', #84300, #77373 ) ;
#40086=EDGE_CURVE ( 'NONE', #98841, #25963, #61587, .T. ) ;
#40087=CIRCLE ( 'NONE', #128033, 5.968999999999998529 ) ;
#40088=ORIENTED_EDGE ( 'NONE', *, *, #70375, .F. ) ;
#40089=DIRECTION ( 'NONE',  ( -0.7071067811865486830, -0.7071067811865464625, -0.000000000000000000 ) ) ;
#40091=ADVANCED_FACE ( 'NONE', ( #62287 ), #126114, .F. ) ;
#40093=DIRECTION ( 'NONE',  ( -0.7071067811865486830, -0.7071067811865464625, 0.000000000000000000 ) ) ;
#40094=CARTESIAN_POINT ( 'NONE',  ( -21.85181644961842196, 17.25929247661554555, 8.802941693769151144 ) ) ;
#40095=DIRECTION ( 'NONE',  ( 0.7071067811865487940, 0.7071067811865463515, -0.000000000000000000 ) ) ;
#40096=DIRECTION ( 'NONE',  ( 0.7071067811865487940, -0.7071067811865463515, 0.000000000000000000 ) ) ;
#40099=AXIS2_PLACEMENT_3D ( 'NONE', #136823, #101340, #1976 ) ;
#40100=ORIENTED_EDGE ( 'NONE', *, *, #57618, .F. ) ;
#40101=CARTESIAN_POINT ( 'NONE',  ( 30.48921356237309510, -27.52281430457076894, 5.000000000000000000 ) ) ;
#40102=DIRECTION ( 'NONE',  ( 0.7071067811865487940, -0.7071067811865463515, 0.000000000000000000 ) ) ;
#40103=EDGE_LOOP ( 'NONE', ( #121982, #36053, #135204 ) ) ;
#40104=EDGE_LOOP ( 'NONE', ( #26142, #19809, #69313, #135112 ) ) ;
#40105=VERTEX_POINT ( 'NONE', #73863 ) ;
#40106=PLANE ( 'NONE',  #65202 ) ;
#40107=CARTESIAN_POINT ( 'NONE',  ( -8.816011393731004731, 28.73617430169781173, 5.000000000000000000 ) ) ;
#40109=ORIENTED_EDGE ( 'NONE', *, *, #42439, .T. ) ;
#40110=PLANE ( 'NONE',  #90252 ) ;
#40111=EDGE_CURVE ( 'NONE', #74550, #45124, #115180, .T. ) ;
#40113=CARTESIAN_POINT ( 'NONE',  ( -23.99451991528749062, 28.92564299267954908, 4.000000000000000000 ) ) ;
#40114=ORIENTED_EDGE ( 'NONE', *, *, #55288, .T. ) ;
#40115=LINE ( 'NONE', #6685, #3474 ) ;
#40116=DIRECTION ( 'NONE',  ( -0.7071067811865487940, 0.7071067811865463515, 0.000000000000000000 ) ) ;
#40117=EDGE_CURVE ( 'NONE', #105516, #39821, #38383, .T. ) ;
#40118=CARTESIAN_POINT ( 'NONE',  ( -60.29974487139158867, -27.71228299555248142, 4.000000000000000000 ) ) ;
#40123=EDGE_LOOP ( 'NONE', ( #129687, #137070, #6464, #33376 ) ) ;
#40124=DIRECTION ( 'NONE',  ( -0.3543493200069162685, -0.000000000000000000, -0.9351131265310288487 ) ) ;
#40125=LINE ( 'NONE', #29203, #65476 ) ;
#40126=CARTESIAN_POINT ( 'NONE',  ( 45.48921356237309510, -27.52281430457087197, 5.000000000000000000 ) ) ;
#40127=VECTOR ( 'NONE', #63097, 1000.000000000000000 ) ;
#40128=EDGE_LOOP ( 'NONE', ( #129967, #12179, #141069, #142947 ) ) ;
#40129=EDGE_CURVE ( 'NONE', #100921, #27961, #6540, .T. ) ;
#40130=ADVANCED_FACE ( 'NONE', ( #4987 ), #118036, .F. ) ;
#40131=FACE_OUTER_BOUND ( 'NONE', #118526, .T. ) ;
#40132=LINE ( 'NONE', #69914, #118206 ) ;
#40133=PLANE ( 'NONE',  #132421 ) ;
#40135=ORIENTED_EDGE ( 'NONE', *, *, #97128, .T. ) ;
#40137=FACE_OUTER_BOUND ( 'NONE', #11439, .T. ) ;
#40138=DIRECTION ( 'NONE',  ( -0.000000000000000000, 0.3543493200069153248, 0.9351131265310292928 ) ) ;
#40140=ADVANCED_FACE ( 'NONE', ( #7128 ), #95602, .F. ) ;
#40141=CARTESIAN_POINT ( 'NONE',  ( 2.816011393730999401, 28.73617430169785436, 5.000000000000000000 ) ) ;
#40142=DIRECTION ( 'NONE',  ( -0.000000000000000000, 0.3543493200069153248, 0.9351131265310292928 ) ) ;
#40143=VERTEX_POINT ( 'NONE', #27479 ) ;
#40144=ORIENTED_EDGE ( 'NONE', *, *, #120067, .F. ) ;
#40145=DIRECTION ( 'NONE',  ( 0.000000000000000000, 0.000000000000000000, -1.000000000000000000 ) ) ;
#40146=DIRECTION ( 'NONE',  ( -0.000000000000000000, 0.3543493200069153248, 0.9351131265310292928 ) ) ;
#40150=LINE ( 'NONE', #104644, #27391 ) ;
#40151=AXIS2_PLACEMENT_3D ( 'NONE', #90781, #59583, #14624 ) ;
#40152=DIRECTION ( 'NONE',  ( -0.3543493200069162685, -0.000000000000000000, -0.9351131265310288487 ) ) ;
#40153=DIRECTION ( 'NONE',  ( -0.000000000000000000, 0.000000000000000000, 1.000000000000000000 ) ) ;
#40154=ORIENTED_EDGE ( 'NONE', *, *, #22805, .T. ) ;
#40155=EDGE_CURVE ( 'NONE', #66046, #96996, #63016, .T. ) ;
#40156=DIRECTION ( 'NONE',  ( -0.7071067811865487940, 0.7071067811865463515, -0.000000000000000000 ) ) ;
#40157=CARTESIAN_POINT ( 'NONE',  ( -16.44665057663207719, 2.259292476615690770, 14.86850063742358330 ) ) ;
#40158=CARTESIAN_POINT ( 'NONE',  ( 29.67183060077626422, 20.25929247661551358, 4.000000000000000000 ) ) ;
#40159=LINE ( 'NONE', #7466, #124713 ) ;
#40162=DIRECTION ( 'NONE',  ( 0.3543493200069162685, -0.000000000000000000, -0.9351131265310288487 ) ) ;
#40163=VERTEX_POINT ( 'NONE', #127525 ) ;
#40164=DIRECTION ( 'NONE',  ( -0.000000000000000000, -0.3543493200069152693, 0.9351131265310292928 ) ) ;
#40165=VECTOR ( 'NONE', #68472, 1000.000000000000000 ) ;
#40166=ORIENTED_EDGE ( 'NONE', *, *, #123106, .T. ) ;
#40167=VERTEX_POINT ( 'NONE', #137709 ) ;
#40168=DIRECTION ( 'NONE',  ( 0.6830127018922180770, -0.6830127018922204085, -0.2588190451025213501 ) ) ;
#40170=DIRECTION ( 'NONE',  ( -0.6830127018922180770, -0.6830127018922204085, -0.2588190451025213501 ) ) ;
#40171=VECTOR ( 'NONE', #2445, 1000.000000000000000 ) ;
#40172=CARTESIAN_POINT ( 'NONE',  ( -16.62823445044374893, -8.240707523384200428, 11.38925528200756432 ) ) ;
#40173=EDGE_CURVE ( 'NONE', #81146, #8053, #107190, .T. ) ;
#40174=CARTESIAN_POINT ( 'NONE',  ( -5.671830600776432973, 20.25929247661551003, 4.000000000000000000 ) ) ;
#40175=CARTESIAN_POINT ( 'NONE',  ( 15.00548008471250228, 28.92564299267927552, 4.000000000000000000 ) ) ;
#40176=ORIENTED_EDGE ( 'NONE', *, *, #139692, .F. ) ;
#40177=LINE ( 'NONE', #95940, #69558 ) ;
#40178=FACE_OUTER_BOUND ( 'NONE', #49801, .T. ) ;
#40179=FACE_OUTER_BOUND ( 'NONE', #14521, .T. ) ;
#40180=LINE ( 'NONE', #16209, #92488 ) ;
#40181=CARTESIAN_POINT ( 'NONE',  ( -15.48921356237309510, -27.52281430457066236, 5.000000000000000000 ) ) ;
#40182=CARTESIAN_POINT ( 'NONE',  ( -72.48921356237309510, -27.52281430457106026, 5.000000000000000000 ) ) ;
#40183=VECTOR ( 'NONE', #125084, 1000.000000000000227 ) ;
#40186=CARTESIAN_POINT ( 'NONE',  ( -0.3281693992235254487, -0.7407075233842788098, 4.000000000000000000 ) ) ;
#40187=ORIENTED_EDGE ( 'NONE', *, *, #88567, .F. ) ;
#40188=ORIENTED_EDGE ( 'NONE', *, *, #72703, .T. ) ;
#40190=DIRECTION ( 'NONE',  ( -0.7071067811865486830, 0.7071067811865464625, 0.000000000000000000 ) ) ;
#40192=AXIS2_PLACEMENT_3D ( 'NONE', #95595, #131095, #42682 ) ;
#40193=ORIENTED_EDGE ( 'NONE', *, *, #94880, .F. ) ;
#40194=EDGE_CURVE ( 'NONE', #101903, #105827, #72481, .T. ) ;
#40195=DIRECTION ( 'NONE',  ( 0.7071067811865487940, -0.7071067811865463515, 0.000000000000000000 ) ) ;
#40196=ADVANCED_FACE ( 'NONE', ( #84058 ), #128256, .F. ) ;
#40198=EDGE_LOOP ( 'NONE', ( #26496, #39372, #16136 ) ) ;
#40199=CARTESIAN_POINT ( 'NONE',  ( -32.99999999999976552, 10.93112307739207445, 4.000000000000000000 ) ) ;
#40201=EDGE_LOOP ( 'NONE', ( #98663, #83148, #72281, #65933 ) ) ;
#40202=VECTOR ( 'NONE', #79931, 1000.000000000000000 ) ;
#40203=CARTESIAN_POINT ( 'NONE',  ( -11.99999999999991296, -18.41253812416056945, 4.000000000000000000 ) ) ;
#40205=FACE_OUTER_BOUND ( 'NONE', #10716, .T. ) ;
#40206=PLANE ( 'NONE',  #11633 ) ;
#40208=LINE ( 'NONE', #72854, #30295 ) ;
#40210=ORIENTED_EDGE ( 'NONE', *, *, #41714, .T. ) ;
#40212=CARTESIAN_POINT ( 'NONE',  ( 1.500000000000001332, 16.08746187583907172, 4.000000000000000000 ) ) ;
#40214=CARTESIAN_POINT ( 'NONE',  ( -12.32816939922343913, 2.259292476615696099, 4.000000000000000000 ) ) ;
#40215=CARTESIAN_POINT ( 'NONE',  ( -6.328169399223481761, -12.74070752338415424, 4.000000000000000000 ) ) ;
#40216=ORIENTED_EDGE ( 'NONE', *, *, #56116, .T. ) ;
#40217=ORIENTED_EDGE ( 'NONE', *, *, #86907, .F. ) ;
#40218=VECTOR ( 'NONE', #94774, 1000.000000000000114 ) ;
#40220=DIRECTION ( 'NONE',  ( 0.7071067811865486830, -0.7071067811865464625, -0.000000000000000000 ) ) ;
#40222=CARTESIAN_POINT ( 'NONE',  ( -34.75611968250420603, 1.705650698524048936, 4.955485411084896263 ) ) ;
#40224=ORIENTED_EDGE ( 'NONE', *, *, #94322, .F. ) ;
#40226=DIRECTION ( 'NONE',  ( -0.3543493200069162685, -0.000000000000000000, -0.9351131265310288487 ) ) ;
#40227=ORIENTED_EDGE ( 'NONE', *, *, #47212, .F. ) ;
#40228=VECTOR ( 'NONE', #22379, 999.9999999999998863 ) ;
#40230=DIRECTION ( 'NONE',  ( -0.6830127018922180770, -0.6830127018922204085, -0.2588190451025213501 ) ) ;
#40231=ORIENTED_EDGE ( 'NONE', *, *, #78503, .F. ) ;
#40232=FACE_OUTER_BOUND ( 'NONE', #65219, .T. ) ;
#40233=FACE_BOUND ( 'NONE', #114941, .T. ) ;
#40234=CARTESIAN_POINT ( 'NONE',  ( 36.29974487139159578, -27.71228299555231445, 4.000000000000000000 ) ) ;
#40235=ADVANCED_FACE ( 'NONE', ( #132564 ), #32510, .F. ) ;
#40236=DIRECTION ( 'NONE',  ( -0.6830127018922180770, -0.6830127018922204085, -0.2588190451025213501 ) ) ;
#40238=CARTESIAN_POINT ( 'NONE',  ( 23.11162361894744777, 9.759292476615614831, 17.35367589129207389 ) ) ;
#40239=ORIENTED_EDGE ( 'NONE', *, *, #134408, .T. ) ;
#40240=VECTOR ( 'NONE', #31314, 1000.000000000000000 ) ;
#40241=ORIENTED_EDGE ( 'NONE', *, *, #27169, .F. ) ;
#40242=ADVANCED_FACE ( 'NONE', ( #74594 ), #108581, .F. ) ;
#40243=ADVANCED_FACE ( 'NONE', ( #140528 ), #9266, .F. ) ;
#40248=PLANE ( 'NONE',  #54547 ) ;
#40249=EDGE_CURVE ( 'NONE', #4447, #59626, #77463, .T. ) ;
#40250=PLANE ( 'NONE',  #69753 ) ;
#40251=EDGE_CURVE ( 'NONE', #39324, #124216, #30352, .T. ) ;
#40252=CARTESIAN_POINT ( 'NONE',  ( 60.18398860626900415, 28.73617430169829490, 5.000000000000000000 ) ) ;
#40253=EDGE_CURVE ( 'NONE', #84947, #67897, #109342, .T. ) ;
#40254=VECTOR ( 'NONE', #43649, 999.9999999999998863 ) ;
#40255=PLANE ( 'NONE',  #35626 ) ;
#40261=DIRECTION ( 'NONE',  ( 0.7071067811865487940, 0.7071067811865463515, 0.000000000000000000 ) ) ;
#40263=LINE ( 'NONE', #6835, #115711 ) ;
#40264=DIRECTION ( 'NONE',  ( 0.7071067811865487940, 0.7071067811865463515, -0.000000000000000000 ) ) ;
#40265=ORIENTED_EDGE ( 'NONE', *, *, #25360, .F. ) ;
#40267=LINE ( 'NONE', #29341, #48910 ) ;
#40268=VECTOR ( 'NONE', #86481, 999.9999999999998863 ) ;
#40269=EDGE_CURVE ( 'NONE', #52145, #3412, #120176, .T. ) ;
#40270=EDGE_LOOP ( 'NONE', ( #139526, #121172, #25907 ) ) ;
#40271=VERTEX_POINT ( 'NONE', #96284 ) ;
#40273=ORIENTED_EDGE ( 'NONE', *, *, #109213, .F. ) ;
#40275=ORIENTED_EDGE ( 'NONE', *, *, #62158, .F. ) ;
#40276=EDGE_CURVE ( 'NONE', #87099, #11206, #65882, .T. ) ;
#40277=AXIS2_PLACEMENT_3D ( 'NONE', #70243, #81817, #70927 ) ;
#40281=ORIENTED_EDGE ( 'NONE', *, *, #118790, .F. ) ;
#40282=DIRECTION ( 'NONE',  ( -0.000000000000000000, 0.3543493200069153248, 0.9351131265310292928 ) ) ;
#40283=VERTEX_POINT ( 'NONE', #10023 ) ;
#40284=VECTOR ( 'NONE', #115680, 1000.000000000000000 ) ;
#40285=CARTESIAN_POINT ( 'NONE',  ( -0.3281693992235289459, -15.74070752338412760, 4.000000000000000000 ) ) ;
#40286=DIRECTION ( 'NONE',  ( -0.7071067811865487940, 0.7071067811865463515, 0.000000000000000000 ) ) ;
#40288=ORIENTED_EDGE ( 'NONE', *, *, #130390, .F. ) ;
#40290=CARTESIAN_POINT ( 'NONE',  ( -1.499999999999994449, -12.08601207473289740, -10.46905243149094389 ) ) ;
#40291=VERTEX_POINT ( 'NONE', #141243 ) ;
#40292=LINE ( 'NONE', #126538, #1774 ) ;
#40293=ORIENTED_EDGE ( 'NONE', *, *, #19415, .F. ) ;
#40294=ORIENTED_EDGE ( 'NONE', *, *, #92590, .F. ) ;
#40295=ORIENTED_EDGE ( 'NONE', *, *, #61919, .T. ) ;
#40296=VERTEX_POINT ( 'NONE', #131101 ) ;
#40297=EDGE_CURVE ( 'NONE', #18088, #40635, #143394, .T. ) ;
#40298=LINE ( 'NONE', #117783, #132814 ) ;
#40299=VECTOR ( 'NONE', #11158, 999.9999999999998863 ) ;
#40300=CARTESIAN_POINT ( 'NONE',  ( 5.816011393731002066, 28.73617430169783304, 5.000000000000000000 ) ) ;
#40301=LINE ( 'NONE', #137452, #97982 ) ;
#40302=LINE ( 'NONE', #84509, #39141 ) ;
#40303=VERTEX_POINT ( 'NONE', #41957 ) ;
#40304=CARTESIAN_POINT ( 'NONE',  ( 26.29289321881328334, -18.74070752338408852, 5.000000000000000000 ) ) ;
#40305=ORIENTED_EDGE ( 'NONE', *, *, #13266, .F. ) ;
#40306=FACE_OUTER_BOUND ( 'NONE', #31900, .T. ) ;
#40307=ADVANCED_FACE ( 'NONE', ( #7865 ), #131818, .T. ) ;
#40308=CARTESIAN_POINT ( 'NONE',  ( 54.18398860626899705, 28.73617430169825226, 5.000000000000000000 ) ) ;
#40309=LINE ( 'NONE', #45140, #27681 ) ;
#40310=AXIS2_PLACEMENT_3D ( 'NONE', #41492, #89127, #52369 ) ;
#40311=ORIENTED_EDGE ( 'NONE', *, *, #15119, .T. ) ;
#40312=LINE ( 'NONE', #77230, #22892 ) ;
#40313=DIRECTION ( 'NONE',  ( -0.3543493200069162685, -0.000000000000000000, -0.9351131265310288487 ) ) ;
#40314=ORIENTED_EDGE ( 'NONE', *, *, #72074, .F. ) ;
#40315=ORIENTED_EDGE ( 'NONE', *, *, #142272, .F. ) ;
#40316=ADVANCED_FACE ( 'NONE', ( #119472 ), #20165, .F. ) ;
#40317=ORIENTED_EDGE ( 'NONE', *, *, #56130, .T. ) ;
#40318=DIRECTION ( 'NONE',  ( -0.000000000000000000, 0.000000000000000000, 1.000000000000000000 ) ) ;
#40319=CARTESIAN_POINT ( 'NONE',  ( -29.24139925780183091, 21.72500000000000853, 5.000000000000000000 ) ) ;
#40320=PLANE ( 'NONE',  #141862 ) ;
#40321=CARTESIAN_POINT ( 'NONE',  ( 12.71757738642558522, -21.73023691814493574, 5.000000000000000888 ) ) ;
#40322=DIRECTION ( 'NONE',  ( 0.7071067811865487940, 0.7071067811865463515, -0.000000000000000000 ) ) ;
#40324=VECTOR ( 'NONE', #78744, 999.9999999999998863 ) ;
#40325=PLANE ( 'NONE',  #122826 ) ;
#40326=CARTESIAN_POINT ( 'NONE',  ( 8.999999999999937828, 15.45873954670186201, -0.03131636524296085855 ) ) ;
#40327=CARTESIAN_POINT ( 'NONE',  ( -0.1839886062690032631, 28.73617430169787568, 5.000000000000000000 ) ) ;
#40329=CARTESIAN_POINT ( 'NONE',  ( 32.99451991528749062, 28.92564299267960948, 4.000000000000000000 ) ) ;
#40330=DIRECTION ( 'NONE',  ( -0.7071067811865487940, 0.7071067811865463515, -0.000000000000000000 ) ) ;
#40331=ORIENTED_EDGE ( 'NONE', *, *, #60372, .T. ) ;
#40333=ORIENTED_EDGE ( 'NONE', *, *, #56706, .T. ) ;
#40334=CYLINDRICAL_SURFACE ( 'NONE', #92378, 0.5000000000000004441 ) ;
#40335=FACE_OUTER_BOUND ( 'NONE', #6702, .T. ) ;
#40336=ORIENTED_EDGE ( 'NONE', *, *, #121689, .F. ) ;
#40337=EDGE_CURVE ( 'NONE', #27137, #74390, #31787, .T. ) ;
#40339=CARTESIAN_POINT ( 'NONE',  ( -4.033400323430202050, 6.759292476615643253, 12.28218704918521453 ) ) ;
#40340=ORIENTED_EDGE ( 'NONE', *, *, #19739, .F. ) ;
#40341=ORIENTED_EDGE ( 'NONE', *, *, #7527, .T. ) ;
#40342=CARTESIAN_POINT ( 'NONE',  ( -3.183988606268992161, 28.73617430169789699, 5.000000000000000000 ) ) ;
#40343=DIRECTION ( 'NONE',  ( -0.6830127018922180770, -0.6830127018922204085, -0.2588190451025213501 ) ) ;
#40344=AXIS2_PLACEMENT_3D ( 'NONE', #77867, #35096, #11861 ) ;
#40345=CARTESIAN_POINT ( 'NONE',  ( 8.994519915287490619, 28.92564299267944250, 4.000000000000000000 ) ) ;
#40347=PLANE ( 'NONE',  #138964 ) ;
#40349=DIRECTION ( 'NONE',  ( -0.6830127018922181881, 0.6830127018922202975, -0.2588190451025214056 ) ) ;
#40350=ORIENTED_EDGE ( 'NONE', *, *, #80178, .T. ) ;
#40351=CARTESIAN_POINT ( 'NONE',  ( 7.499999999999961808, 19.08746187583905396, 4.000000000000000000 ) ) ;
#40352=EDGE_CURVE ( 'NONE', #116152, #112560, #120925, .T. ) ;
#40355=LINE ( 'NONE', #84564, #35200 ) ;
#40356=VERTEX_POINT ( 'NONE', #36088 ) ;
#40357=EDGE_CURVE ( 'NONE', #20616, #114574, #101320, .T. ) ;
#40358=EDGE_CURVE ( 'NONE', #78905, #7428, #89044, .T. ) ;
#40359=FACE_OUTER_BOUND ( 'NONE', #136343, .T. ) ;
#40360=ORIENTED_EDGE ( 'NONE', *, *, #42969, .F. ) ;
#40361=ADVANCED_FACE ( 'NONE', ( #2707 ), #123814, .F. ) ;
#40362=VECTOR ( 'NONE', #47115, 1000.000000000000000 ) ;
#40363=VECTOR ( 'NONE', #1617, 1000.000000000000114 ) ;
#40365=CARTESIAN_POINT ( 'NONE',  ( 32.99451991528749062, 28.92564299267960948, 4.000000000000000000 ) ) ;
#40366=CARTESIAN_POINT ( 'NONE',  ( -32.20710678118631165, -11.24070752338416668, 5.000000000000000000 ) ) ;
#40367=PLANE ( 'NONE',  #121967 ) ;
#40368=ORIENTED_EDGE ( 'NONE', *, *, #107641, .T. ) ;
#40369=PLANE ( 'NONE',  #69802 ) ;
#40370=DIRECTION ( 'NONE',  ( 0.7071067811865487940, -0.7071067811865463515, 0.000000000000000000 ) ) ;
#40371=VECTOR ( 'NONE', #137088, 999.9999999999998863 ) ;
#40372=LINE ( 'NONE', #4797, #115631 ) ;
#40373=EDGE_CURVE ( 'NONE', #133213, #96656, #1955, .T. ) ;
#40374=CARTESIAN_POINT ( 'NONE',  ( -7.641757024588559766, 15.75929247661555088, 19.34181609438701344 ) ) ;
#40375=ORIENTED_EDGE ( 'NONE', *, *, #92265, .F. ) ;
#40377=CARTESIAN_POINT ( 'NONE',  ( -66.48921356237309510, -27.52281430457101763, 5.000000000000000000 ) ) ;
#40379=AXIS2_PLACEMENT_3D ( 'NONE', #62389, #117428, #20989 ) ;
#40380=ORIENTED_EDGE ( 'NONE', *, *, #52177, .F. ) ;
#40383=VECTOR ( 'NONE', #108873, 1000.000000000000000 ) ;
#40385=DIRECTION ( 'NONE',  ( 0.7071067811865487940, 0.7071067811865463515, -0.000000000000000000 ) ) ;
#40386=FACE_OUTER_BOUND ( 'NONE', #66846, .T. ) ;
#40387=CARTESIAN_POINT ( 'NONE',  ( 3.183988606268992161, 28.73617430169789699, 5.000000000000000000 ) ) ;
#40388=VERTEX_POINT ( 'NONE', #23010 ) ;
#40389=DIRECTION ( 'NONE',  ( -0.7071067811865487940, 0.7071067811865463515, -0.000000000000000000 ) ) ;
#40392=ORIENTED_EDGE ( 'NONE', *, *, #40593, .F. ) ;
#40395=LINE ( 'NONE', #84601, #84079 ) ;
#40396=ORIENTED_EDGE ( 'NONE', *, *, #109906, .F. ) ;
#40397=ORIENTED_EDGE ( 'NONE', *, *, #116056, .T. ) ;
#40398=ADVANCED_FACE ( 'NONE', ( #33941 ), #12860, .F. ) ;
#40403=CARTESIAN_POINT ( 'NONE',  ( 27.18398860626900060, 28.73617430169806042, 5.000000000000000000 ) ) ;
#40404=VERTEX_POINT ( 'NONE', #69430 ) ;
#40408=ADVANCED_FACE ( 'NONE', ( #11416 ), #68716, .T. ) ;
#40409=ORIENTED_EDGE ( 'NONE', *, *, #108991, .T. ) ;
#40410=EDGE_CURVE ( 'NONE', #33542, #67920, #90449, .T. ) ;
#40412=EDGE_CURVE ( 'NONE', #106956, #75231, #112909, .T. ) ;
#40413=VECTOR ( 'NONE', #65949, 1000.000000000000114 ) ;
#40416=EDGE_LOOP ( 'NONE', ( #52883, #55444, #112631, #2233 ) ) ;
#40418=FACE_OUTER_BOUND ( 'NONE', #15559, .T. ) ;
#40425=EDGE_CURVE ( 'NONE', #81393, #119020, #133261, .T. ) ;
#40426=EDGE_LOOP ( 'NONE', ( #127186, #69860, #65103, #68265 ) ) ;
#40428=CARTESIAN_POINT ( 'NONE',  ( 48.18398860626899705, 28.73617430169820608, 5.000000000000000000 ) ) ;
#40429=ORIENTED_EDGE ( 'NONE', *, *, #131724, .F. ) ;
#40431=DIRECTION ( 'NONE',  ( -0.7071067811865486830, -0.7071067811865464625, -0.000000000000000000 ) ) ;
#40432=EDGE_LOOP ( 'NONE', ( #117011, #92339, #69639, #7405 ) ) ;
#40435=ORIENTED_EDGE ( 'NONE', *, *, #122239, .F. ) ;
#40437=ADVANCED_FACE ( 'NONE', ( #14308 ), #134695, .F. ) ;
#40438=CARTESIAN_POINT ( 'NONE',  ( 8.816011393731004731, 28.73617430169781173, 5.000000000000000000 ) ) ;
#40440=LINE ( 'NONE', #118684, #31154 ) ;
#40443=DIRECTION ( 'NONE',  ( 0.6830127018922180770, -0.6830127018922204085, -0.2588190451025213501 ) ) ;
#40445=CARTESIAN_POINT ( 'NONE',  ( 33.29974487139158867, -27.71228299555229313, 4.000000000000000000 ) ) ;
#40446=DIRECTION ( 'NONE',  ( 0.7071067811865486830, -0.7071067811865464625, -0.000000000000000000 ) ) ;
#40447=EDGE_CURVE ( 'NONE', #1803, #130345, #78158, .T. ) ;
#40448=LINE ( 'NONE', #4886, #142599 ) ;
#40449=LINE ( 'NONE', #60795, #81765 ) ;
#40450=LINE ( 'NONE', #42600, #37529 ) ;
#40451=LINE ( 'NONE', #118693, #26587 ) ;
#40452=ORIENTED_EDGE ( 'NONE', *, *, #113999, .F. ) ;
#40453=DIRECTION ( 'NONE',  ( 0.7071067811865487940, -0.7071067811865463515, 0.000000000000000000 ) ) ;
#40455=ORIENTED_EDGE ( 'NONE', *, *, #102274, .T. ) ;
#40456=VERTEX_POINT ( 'NONE', #88260 ) ;
#40457=EDGE_LOOP ( 'NONE', ( #32841, #85665, #125263, #41918 ) ) ;
#40458=EDGE_CURVE ( 'NONE', #87786, #22970, #90386, .T. ) ;
#40459=ORIENTED_EDGE ( 'NONE', *, *, #14401, .T. ) ;
#40460=CARTESIAN_POINT ( 'NONE',  ( -5.758305415748097289, 0.7592924766157034266, 14.37146558664984042 ) ) ;
#40461=CARTESIAN_POINT ( 'NONE',  ( 34.47516574401891631, -14.97193265888402713, 4.998110765256834398 ) ) ;
#40462=CARTESIAN_POINT ( 'NONE',  ( 0.000000000000000000, 0.000000000000000000, 5.000000000000000000 ) ) ;
#40463=CARTESIAN_POINT ( 'NONE',  ( 0.000000000000000000, 0.000000000000000000, 5.000000000000000000 ) ) ;
#40464=ORIENTED_EDGE ( 'NONE', *, *, #34838, .F. ) ;
#40466=ORIENTED_EDGE ( 'NONE', *, *, #60800, .T. ) ;
#40467=EDGE_CURVE ( 'NONE', #65577, #135321, #140791, .T. ) ;
#40471=VECTOR ( 'NONE', #16538, 1000.000000000000000 ) ;
#40472=DIRECTION ( 'NONE',  ( -0.000000000000000000, 0.000000000000000000, 1.000000000000000000 ) ) ;
#40473=VECTOR ( 'NONE', #68765, 1000.000000000000000 ) ;
#40474=LINE ( 'NONE', #82533, #2722 ) ;
#40475=ORIENTED_EDGE ( 'NONE', *, *, #142835, .T. ) ;
#40476=ORIENTED_EDGE ( 'NONE', *, *, #80269, .T. ) ;
#40477=EDGE_CURVE ( 'NONE', #104186, #4701, #68663, .T. ) ;
#40478=ORIENTED_EDGE ( 'NONE', *, *, #43035, .T. ) ;
#40481=DIRECTION ( 'NONE',  ( -0.7071067811865487940, 0.7071067811865463515, -0.000000000000000000 ) ) ;
#40484=CARTESIAN_POINT ( 'NONE',  ( -10.49999999999993250, 1.030536316426501564, -5.498701923753775311 ) ) ;
#40487=EDGE_CURVE ( 'NONE', #121873, #121929, #22949, .T. ) ;
#40488=CARTESIAN_POINT ( 'NONE',  ( 34.92499999999998295, -22.22500000000000142, 4.500000000000000888 ) ) ;
#40489=ORIENTED_EDGE ( 'NONE', *, *, #29440, .T. ) ;
#40490=DIRECTION ( 'NONE',  ( 0.7071067811865487940, -0.7071067811865463515, -0.000000000000000000 ) ) ;
#40491=CARTESIAN_POINT ( 'NONE',  ( 0.000000000000000000, 0.000000000000000000, 5.000000000000000000 ) ) ;
#40492=VERTEX_POINT ( 'NONE', #88983 ) ;
#40493=CARTESIAN_POINT ( 'NONE',  ( 26.29320749275909463, 20.25929247661551358, 20.83292124670808931 ) ) ;
#40494=PLANE ( 'NONE',  #74267 ) ;
#40495=VERTEX_POINT ( 'NONE', #1210 ) ;
#40497=DIRECTION ( 'NONE',  ( 0.3543493200069162685, -0.000000000000000000, -0.9351131265310288487 ) ) ;
#40499=EDGE_LOOP ( 'NONE', ( #88887, #10491, #53522, #82832, #96518 ) ) ;
#40500=CARTESIAN_POINT ( 'NONE',  ( -19.49999999999986500, 9.127013188829483425, 4.802533355213530086 ) ) ;
#40501=ORIENTED_EDGE ( 'NONE', *, *, #79326, .T. ) ;
#40505=FACE_OUTER_BOUND ( 'NONE', #20722, .T. ) ;
#40506=FACE_OUTER_BOUND ( 'NONE', #136075, .T. ) ;
#40507=LINE ( 'NONE', #128227, #131653 ) ;
#40510=LINE ( 'NONE', #84712, #14260 ) ;
#40511=DIRECTION ( 'NONE',  ( 0.3543493200069162685, -0.000000000000000000, -0.9351131265310288487 ) ) ;
#40512=ORIENTED_EDGE ( 'NONE', *, *, #96496, .F. ) ;
#40513=VECTOR ( 'NONE', #67929, 1000.000000000000000 ) ;
#40514=EDGE_LOOP ( 'NONE', ( #60014, #2495, #115432, #2681 ) ) ;
#40516=CARTESIAN_POINT ( 'NONE',  ( 0.000000000000000000, 0.000000000000000000, 5.000000000000000000 ) ) ;
#40517=ORIENTED_EDGE ( 'NONE', *, *, #142641, .F. ) ;
#40518=EDGE_CURVE ( 'NONE', #80227, #20476, #115022, .T. ) ;
#40520=CARTESIAN_POINT ( 'NONE',  ( -15.18398860626900237, 28.73617430169797871, 5.000000000000000000 ) ) ;
#40522=EDGE_LOOP ( 'NONE', ( #28338, #86332, #62396, #122385 ) ) ;
#40523=CARTESIAN_POINT ( 'NONE',  ( -34.49999999999976552, 3.054329344830908344, 4.994342998332172101 ) ) ;
#40524=DIRECTION ( 'NONE',  ( 0.6830127018922180770, -0.6830127018922204085, -0.2588190451025213501 ) ) ;
#40525=CARTESIAN_POINT ( 'NONE',  ( 4.499999999999966249, 14.14708470758591652, -0.5283514160166653539 ) ) ;
#40526=EDGE_CURVE ( 'NONE', #11525, #35337, #23704, .T. ) ;
#40529=DIRECTION ( 'NONE',  ( 1.000000000000000000, 0.000000000000000000, 0.000000000000000000 ) ) ;
#40531=CARTESIAN_POINT ( 'NONE',  ( 30.70612307739174796, 22.22500000000000142, 4.000000000000000000 ) ) ;
#40532=CARTESIAN_POINT ( 'NONE',  ( 30.32816939922332367, 17.25929247661554200, 4.000000000000000000 ) ) ;
#40533=PLANE ( 'NONE',  #86351 ) ;
#40534=DIRECTION ( 'NONE',  ( -0.000000000000000000, 0.3543493200069153248, 0.9351131265310292928 ) ) ;
#40535=LINE ( 'NONE', #1088, #119291 ) ;
#40537=VECTOR ( 'NONE', #92556, 1000.000000000000227 ) ;
#40539=EDGE_LOOP ( 'NONE', ( #81856, #23693, #60210, #12545 ) ) ;
#40541=ORIENTED_EDGE ( 'NONE', *, *, #105201, .T. ) ;
#40542=VECTOR ( 'NONE', #43370, 1000.000000000000000 ) ;
#40544=CARTESIAN_POINT ( 'NONE',  ( 6.707106781186499944, -12.74070752338415247, 5.000000000000000000 ) ) ;
#40545=VERTEX_POINT ( 'NONE', #69373 ) ;
#40546=EDGE_CURVE ( 'NONE', #37549, #4136, #110674, .T. ) ;
#40547=CARTESIAN_POINT ( 'NONE',  ( -30.48921356237309510, -27.52281430457076894, 5.000000000000000000 ) ) ;
#40548=CARTESIAN_POINT ( 'NONE',  ( 50.99451991528749062, 28.92564299267973738, 4.000000000000000000 ) ) ;
#40551=ORIENTED_EDGE ( 'NONE', *, *, #23521, .T. ) ;
#40553=DIRECTION ( 'NONE',  ( 0.7071067811865486830, -0.7071067811865464625, -0.000000000000000000 ) ) ;
#40554=ORIENTED_EDGE ( 'NONE', *, *, #114039, .T. ) ;
#40555=DIRECTION ( 'NONE',  ( 0.7071067811865486830, -0.7071067811865464625, -0.000000000000000000 ) ) ;
#40557=PLANE ( 'NONE',  #113356 ) ;
#40558=ORIENTED_EDGE ( 'NONE', *, *, #46698, .F. ) ;
#40559=ORIENTED_EDGE ( 'NONE', *, *, #68787, .F. ) ;
#40560=ORIENTED_EDGE ( 'NONE', *, *, #94197, .T. ) ;
#40561=CARTESIAN_POINT ( 'NONE',  ( 23.67183060077631396, 14.25929247661558286, 4.000000000000000000 ) ) ;
#40562=CARTESIAN_POINT ( 'NONE',  ( 53.99451991528749062, 28.92564299267975869, 4.000000000000000000 ) ) ;
#40565=VECTOR ( 'NONE', #101117, 1000.000000000000000 ) ;
#40567=AXIS2_PLACEMENT_3D ( 'NONE', #122806, #280, #47446 ) ;
#40568=AXIS2_PLACEMENT_3D ( 'NONE', #109955, #23669, #67941 ) ;
#40569=EDGE_CURVE ( 'NONE', #20459, #59056, #55633, .T. ) ;
#40570=VERTEX_POINT ( 'NONE', #99835 ) ;
#40571=VECTOR ( 'NONE', #78585, 1000.000000000000000 ) ;
#40572=ORIENTED_EDGE ( 'NONE', *, *, #13836, .T. ) ;
#40575=LINE ( 'NONE', #129688, #128905 ) ;
#40576=ORIENTED_EDGE ( 'NONE', *, *, #44502, .T. ) ;
#40577=VERTEX_POINT ( 'NONE', #99091 ) ;
#40578=EDGE_CURVE ( 'NONE', #65015, #120961, #33882, .T. ) ;
#40580=CARTESIAN_POINT ( 'NONE',  ( 35.99451991528749772, 28.92564299267963079, 4.000000000000000000 ) ) ;
#40581=ORIENTED_EDGE ( 'NONE', *, *, #116947, .T. ) ;
#40583=FACE_OUTER_BOUND ( 'NONE', #83846, .T. ) ;
#40584=DIRECTION ( 'NONE',  ( 0.7071067811865487940, 0.7071067811865463515, 0.000000000000000000 ) ) ;
#40585=FACE_OUTER_BOUND ( 'NONE', #22661, .T. ) ;
#40586=VERTEX_POINT ( 'NONE', #89670 ) ;
#40587=LINE ( 'NONE', #29674, #53334 ) ;
#40589=EDGE_CURVE ( 'NONE', #63037, #99871, #135351, .T. ) ;
#40590=VERTEX_POINT ( 'NONE', #124444 ) ;
#40591=CARTESIAN_POINT ( 'NONE',  ( -32.99451991528749062, 28.92564299267960948, 4.000000000000000000 ) ) ;
#40592=DIRECTION ( 'NONE',  ( -0.000000000000000000, 0.000000000000000000, 1.000000000000000000 ) ) ;
#40593=EDGE_CURVE ( 'NONE', #112076, #113191, #111415, .T. ) ;
#40594=EDGE_LOOP ( 'NONE', ( #134080, #51435, #83585, #26810 ) ) ;
#40595=CARTESIAN_POINT ( 'NONE',  ( 24.29974487139158867, -27.71228299555223273, 4.000000000000000000 ) ) ;
#40596=ORIENTED_EDGE ( 'NONE', *, *, #12360, .F. ) ;
#40597=ORIENTED_EDGE ( 'NONE', *, *, #21542, .T. ) ;
#40598=ORIENTED_EDGE ( 'NONE', *, *, #122242, .T. ) ;
#40601=CARTESIAN_POINT ( 'NONE',  ( 34.49999999999975842, 10.46425560840038571, 4.994342998332157890 ) ) ;
#40602=LINE ( 'NONE', #96354, #132900 ) ;
#40603=CARTESIAN_POINT ( 'NONE',  ( 0.000000000000000000, 0.000000000000000000, 5.000000000000000000 ) ) ;
#40604=LINE ( 'NONE', #5784, #109923 ) ;
#40605=PLANE ( 'NONE',  #71430 ) ;
#40607=CARTESIAN_POINT ( 'NONE',  ( -17.24139925780192328, 21.72500000000000142, 5.000000000000000000 ) ) ;
#40608=EDGE_CURVE ( 'NONE', #14910, #69767, #44039, .T. ) ;
#40609=PLANE ( 'NONE',  #74822 ) ;
#40610=DIRECTION ( 'NONE',  ( 0.7071067811865487940, -0.7071067811865463515, 0.000000000000000000 ) ) ;
#40611=DIRECTION ( 'NONE',  ( -0.7071067811865486830, 0.7071067811865464625, 0.000000000000000000 ) ) ;
#40612=DIRECTION ( 'NONE',  ( 0.7071067811865487940, 0.7071067811865463515, 0.000000000000000000 ) ) ;
#40613=ORIENTED_EDGE ( 'NONE', *, *, #8789, .F. ) ;
#40614=ORIENTED_EDGE ( 'NONE', *, *, #65947, .T. ) ;
#40616=ORIENTED_EDGE ( 'NONE', *, *, #53400, .F. ) ;
#40617=ORIENTED_EDGE ( 'NONE', *, *, #98817, .F. ) ;
#40619=ORIENTED_EDGE ( 'NONE', *, *, #72988, .F. ) ;
#40621=CARTESIAN_POINT ( 'NONE',  ( -21.18398860626899349, 28.73617430169802134, 5.000000000000000000 ) ) ;
#40623=CARTESIAN_POINT ( 'NONE',  ( 10.49999999999992895, -4.533600742197696043, 5.000000000000000000 ) ) ;
#40624=CARTESIAN_POINT ( 'NONE',  ( -10.49999999999991829, 1.087461875839235814, 4.000000000000000000 ) ) ;
#40625=EDGE_CURVE ( 'NONE', #29676, #129956, #4031, .T. ) ;
#40626=ORIENTED_EDGE ( 'NONE', *, *, #106814, .T. ) ;
#40627=ADVANCED_FACE ( 'NONE', ( #71507 ), #27994, .F. ) ;
#40631=EDGE_CURVE ( 'NONE', #11751, #101542, #6192, .T. ) ;
#40632=AXIS2_PLACEMENT_3D ( 'NONE', #111290, #88144, #31616 ) ;
#40633=DIRECTION ( 'NONE',  ( 0.7071067811865486830, -0.7071067811865464625, -0.000000000000000000 ) ) ;
#40635=VERTEX_POINT ( 'NONE', #25845 ) ;
#40637=AXIS2_PLACEMENT_3D ( 'NONE', #134520, #11990, #121474 ) ;
#40639=ORIENTED_EDGE ( 'NONE', *, *, #77275, .T. ) ;
#40640=ORIENTED_EDGE ( 'NONE', *, *, #34196, .F. ) ;
#40641=DIRECTION ( 'NONE',  ( -0.7071067811865487940, 0.7071067811865463515, -0.000000000000000000 ) ) ;
#40642=ORIENTED_EDGE ( 'NONE', *, *, #132781, .T. ) ;
#40643=CARTESIAN_POINT ( 'NONE',  ( 18.32816939922339472, -15.74070752338412760, 4.000000000000000000 ) ) ;
#40644=LINE ( 'NONE', #107990, #11686 ) ;
#40645=PLANE ( 'NONE',  #53983 ) ;
#40646=LINE ( 'NONE', #74715, #26371 ) ;
#40647=ORIENTED_EDGE ( 'NONE', *, *, #129751, .T. ) ;
#40648=CARTESIAN_POINT ( 'NONE',  ( -5.994519915287488843, 28.92564299267942118, 4.000000000000000000 ) ) ;
#40650=CARTESIAN_POINT ( 'NONE',  ( -26.99451991528749417, 28.92564299267956685, 4.000000000000000000 ) ) ;
#40651=PLANE ( 'NONE',  #5150 ) ;
#40652=ORIENTED_EDGE ( 'NONE', *, *, #32883, .T. ) ;
#40654=CARTESIAN_POINT ( 'NONE',  ( 12.48921356237309155, -27.52281430457064104, 5.000000000000000000 ) ) ;
#40656=DIRECTION ( 'NONE',  ( -0.6830127018922181881, 0.6830127018922202975, -0.2588190451025214056 ) ) ;
#40657=ORIENTED_EDGE ( 'NONE', *, *, #69358, .T. ) ;
#40658=ORIENTED_EDGE ( 'NONE', *, *, #100702, .T. ) ;
#40659=CARTESIAN_POINT ( 'NONE',  ( 19.49999999999986500, -6.839392718269110105, -8.480912228396132235 ) ) ;
#40660=CARTESIAN_POINT ( 'NONE',  ( -3.183988606268992161, 28.73617430169789699, 5.000000000000000000 ) ) ;
#40661=ORIENTED_EDGE ( 'NONE', *, *, #80992, .T. ) ;
#40662=PLANE ( 'NONE',  #51190 ) ;
#40663=VECTOR ( 'NONE', #36939, 1000.000000000000000 ) ;
#40664=DIRECTION ( 'NONE',  ( -0.000000000000000000, 0.3543493200069153248, 0.9351131265310292928 ) ) ;
#40665=VECTOR ( 'NONE', #376, 1000.000000000000000 ) ;
#40666=DIRECTION ( 'NONE',  ( 0.6830127018922180770, -0.6830127018922202975, -0.2588190451025213501 ) ) ;
#40667=VECTOR ( 'NONE', #135660, 1000.000000000000000 ) ;
#40668=CARTESIAN_POINT ( 'NONE',  ( -36.18398860626899705, 28.73617430169812437, 5.000000000000000000 ) ) ;
#40670=LINE ( 'NONE', #98598, #16539 ) ;
#40672=FACE_OUTER_BOUND ( 'NONE', #74711, .T. ) ;
#40673=CARTESIAN_POINT ( 'NONE',  ( 57.29974487139158157, -27.71228299555246011, 4.000000000000000000 ) ) ;
#40674=DIRECTION ( 'NONE',  ( -0.3543493200069162685, -0.000000000000000000, -0.9351131265310288487 ) ) ;
#40675=CARTESIAN_POINT ( 'NONE',  ( 28.17183060077628554, 21.75929247661550647, 4.000000000000000000 ) ) ;
#40676=AXIS2_PLACEMENT_3D ( 'NONE', #4756, #93250, #105536 ) ;
#40677=CARTESIAN_POINT ( 'NONE',  ( 75.18398860626899705, 28.73617430169839793, 5.000000000000000000 ) ) ;
#40679=ORIENTED_EDGE ( 'NONE', *, *, #66742, .T. ) ;
#40680=EDGE_LOOP ( 'NONE', ( #57257, #84799, #60979, #40823 ) ) ;
#40681=ORIENTED_EDGE ( 'NONE', *, *, #121887, .F. ) ;
#40683=ORIENTED_EDGE ( 'NONE', *, *, #36228, .F. ) ;
#40684=EDGE_LOOP ( 'NONE', ( #135649, #11218, #17715, #108486 ) ) ;
#40685=ORIENTED_EDGE ( 'NONE', *, *, #142523, .T. ) ;
#40686=CARTESIAN_POINT ( 'NONE',  ( -48.29974487139158867, -27.71228299555239971, 4.000000000000000000 ) ) ;
#40687=CARTESIAN_POINT ( 'NONE',  ( 45.48921356237309510, -27.52281430457087197, 5.000000000000000000 ) ) ;
#40688=EDGE_LOOP ( 'NONE', ( #106787, #75165, #40336, #80229 ) ) ;
#40689=LINE ( 'NONE', #94336, #50916 ) ;
#40690=LINE ( 'NONE', #52263, #108841 ) ;
#40691=DIRECTION ( 'NONE',  ( 0.7071067811865487940, -0.7071067811865463515, 0.000000000000000000 ) ) ;
#40692=CARTESIAN_POINT ( 'NONE',  ( -34.49999999999976552, -1.535744391599501490, 4.994342998332164996 ) ) ;
#40694=EDGE_CURVE ( 'NONE', #52896, #59390, #70120, .T. ) ;
#40695=VERTEX_POINT ( 'NONE', #72263 ) ;
#40696=CARTESIAN_POINT ( 'NONE',  ( 30.18398860626900060, 28.73617430169808173, 5.000000000000000000 ) ) ;
#40697=CARTESIAN_POINT ( 'NONE',  ( 25.49999999999982592, 3.653845994658417418, -4.504631822206428993 ) ) ;
#40698=EDGE_CURVE ( 'NONE', #77145, #104436, #72969, .T. ) ;
#40699=CARTESIAN_POINT ( 'NONE',  ( -25.49999999999982592, 11.52377502935400599, -1.522421517564026772 ) ) ;
#40700=CARTESIAN_POINT ( 'NONE',  ( 15.68879807097514956, -1.757674993583058898, 4.000000000000000000 ) ) ;
#40702=DIRECTION ( 'NONE',  ( 0.7071067811865487940, 0.7071067811865463515, 0.000000000000000000 ) ) ;
#40704=CARTESIAN_POINT ( 'NONE',  ( -26.99999999999981171, -7.068876922607739921, 4.000000000000000000 ) ) ;
#40706=DIRECTION ( 'NONE',  ( -0.7071067811865486830, -0.7071067811865464625, -0.000000000000000000 ) ) ;
#40707=ORIENTED_EDGE ( 'NONE', *, *, #15024, .F. ) ;
#40708=ORIENTED_EDGE ( 'NONE', *, *, #92270, .F. ) ;
#40710=EDGE_LOOP ( 'NONE', ( #3464, #23065, #132038, #83784 ) ) ;
#40711=EDGE_CURVE ( 'NONE', #83776, #80177, #17118, .T. ) ;
#40712=DIRECTION ( 'NONE',  ( 0.7071067811865486830, -0.7071067811865464625, -0.000000000000000000 ) ) ;
#40713=CARTESIAN_POINT ( 'NONE',  ( -3.489213562373097322, -27.52281430457057709, 5.000000000000000000 ) ) ;
#40714=FACE_OUTER_BOUND ( 'NONE', #114285, .T. ) ;
#40715=CARTESIAN_POINT ( 'NONE',  ( -22.49999999999984723, 19.39370406404965408, 1.459788787078254657 ) ) ;
#40716=ADVANCED_FACE ( 'NONE', ( #114282 ), #83838, .F. ) ;
#40717=CARTESIAN_POINT ( 'NONE',  ( -9.183988606268997046, 28.73617430169793607, 5.000000000000000000 ) ) ;
#40718=LINE ( 'NONE', #84924, #114 ) ;
#40720=VERTEX_POINT ( 'NONE', #136737 ) ;
#40721=DIRECTION ( 'NONE',  ( 0.7071067811865486830, -0.7071067811865464625, -0.000000000000000000 ) ) ;
#40722=ORIENTED_EDGE ( 'NONE', *, *, #72378, .T. ) ;
#40723=FACE_OUTER_BOUND ( 'NONE', #80793, .T. ) ;
#40724=EDGE_CURVE ( 'NONE', #96207, #89805, #138187, .T. ) ;
#40725=CARTESIAN_POINT ( 'NONE',  ( -13.80981832425542954, -18.74070752338408852, 7.910009926591540008 ) ) ;
#40727=( BOUNDED_CURVE ( )  B_SPLINE_CURVE ( 3, ( #71052, #56091, #89390, #33613 ),
 .UNSPECIFIED., .F., .T. ) 
 B_SPLINE_CURVE_WITH_KNOTS ( ( 4, 4 ),
 ( 4.350170835173029715, 4.500739107949200069 ),
 .UNSPECIFIED. ) 
 CURVE ( )  GEOMETRIC_REPRESENTATION_ITEM ( )  RATIONAL_B_SPLINE_CURVE ( ( 1.000000000000000000, 0.9981116584018959736, 0.9981116584018959736, 1.000000000000000000 ) ) 
 REPRESENTATION_ITEM ( '' )  );
#40728=LINE ( 'NONE', #74064, #9345 ) ;
#40729=VERTEX_POINT ( 'NONE', #4748 ) ;
#40731=EDGE_LOOP ( 'NONE', ( #103639, #99539, #10078, #75918 ) ) ;
#40733=DIRECTION ( 'NONE',  ( -0.7071067811865487940, 0.7071067811865463515, -0.000000000000000000 ) ) ;
#40734=PLANE ( 'NONE',  #82562 ) ;
#40735=EDGE_CURVE ( 'NONE', #113219, #108055, #126567, .T. ) ;
#40736=CARTESIAN_POINT ( 'NONE',  ( -2.994519915287485734, 28.92564299267940342, 4.000000000000000000 ) ) ;
#40737=VECTOR ( 'NONE', #38404, 1000.000000000000000 ) ;
#40739=EDGE_LOOP ( 'NONE', ( #88976, #77739, #55258, #63137, #29187 ) ) ;
#40740=AXIS2_PLACEMENT_3D ( 'NONE', #111875, #122003, #99534 ) ;
#40741=EDGE_CURVE ( 'NONE', #57945, #30286, #58538, .T. ) ;
#40742=DIRECTION ( 'NONE',  ( -0.6830127018922180770, -0.6830127018922204085, -0.2588190451025213501 ) ) ;
#40743=EDGE_LOOP ( 'NONE', ( #46907, #89100, #4034, #77700 ) ) ;
#40744=ORIENTED_EDGE ( 'NONE', *, *, #112172, .T. ) ;
#40745=EDGE_LOOP ( 'NONE', ( #68473, #41778, #56653, #142968 ) ) ;
#40746=EDGE_CURVE ( 'NONE', #93317, #73359, #115668, .T. ) ;
#40749=DIRECTION ( 'NONE',  ( -0.7071067811865486830, -0.7071067811865464625, 0.000000000000000000 ) ) ;
#40751=LINE ( 'NONE', #29841, #4234 ) ;
#40752=AXIS2_PLACEMENT_3D ( 'NONE', #89520, #24955, #66361 ) ;
#40753=LINE ( 'NONE', #8764, #29744 ) ;
#40754=EDGE_CURVE ( 'NONE', #41681, #130550, #93245, .T. ) ;
#40756=FACE_BOUND ( 'NONE', #66190, .T. ) ;
#40757=EDGE_CURVE ( 'NONE', #37138, #81345, #136030, .T. ) ;
#40758=ORIENTED_EDGE ( 'NONE', *, *, #141487, .T. ) ;
#40759=DIRECTION ( 'NONE',  ( 0.7071067811865487940, 0.7071067811865463515, -0.000000000000000000 ) ) ;
#40760=CARTESIAN_POINT ( 'NONE',  ( -34.49999999999975842, 22.21934299833216997, 4.348028800457638177 ) ) ;
#40761=DIRECTION ( 'NONE',  ( 0.6830127018922181881, 0.6830127018922202975, -0.2588190451025214056 ) ) ;
#40762=ADVANCED_FACE ( 'NONE', ( #37455 ), #125893, .F. ) ;
#40763=EDGE_LOOP ( 'NONE', ( #107780, #53815, #11996, #121834 ) ) ;
#40765=ORIENTED_EDGE ( 'NONE', *, *, #22329, .F. ) ;
#40766=EDGE_LOOP ( 'NONE', ( #37367, #51210, #139036 ) ) ;
#40767=FACE_OUTER_BOUND ( 'NONE', #76613, .T. ) ;
#40768=VECTOR ( 'NONE', #68033, 1000.000000000000000 ) ;
#40769=ORIENTED_EDGE ( 'NONE', *, *, #28023, .T. ) ;
#40770=AXIS2_PLACEMENT_3D ( 'NONE', #8900, #187, #20526 ) ;
#40772=ORIENTED_EDGE ( 'NONE', *, *, #84240, .F. ) ;
#40773=EDGE_CURVE ( 'NONE', #70580, #101203, #104090, .T. ) ;
#40774=LINE ( 'NONE', #6651, #108918 ) ;
#40775=VECTOR ( 'NONE', #59452, 1000.000000000000000 ) ;
#40776=CARTESIAN_POINT ( 'NONE',  ( -23.99451991528749062, 28.92564299267954908, 4.000000000000000000 ) ) ;
#40777=ORIENTED_EDGE ( 'NONE', *, *, #53610, .T. ) ;
#40778=PLANE ( 'NONE',  #49171 ) ;
#40779=VECTOR ( 'NONE', #140675, 999.9999999999998863 ) ;
#40780=EDGE_CURVE ( 'NONE', #96557, #137344, #85938, .T. ) ;
#40781=DIRECTION ( 'NONE',  ( -0.6830127018922180770, -0.6830127018922204085, -0.2588190451025213501 ) ) ;
#40782=DIRECTION ( 'NONE',  ( 4.681814790819592407E-17, 0.3543493200069153248, 0.9351131265310292928 ) ) ;
#40783=CARTESIAN_POINT ( 'NONE',  ( 15.48921356237309510, -27.52281430457066236, 5.000000000000000000 ) ) ;
#40784=CARTESIAN_POINT ( 'NONE',  ( 34.92499999999998295, -21.18334561358932433, 4.500000000000000888 ) ) ;
#40786=ORIENTED_EDGE ( 'NONE', *, *, #13155, .F. ) ;
#40787=ORIENTED_EDGE ( 'NONE', *, *, #64059, .F. ) ;
#40788=DIRECTION ( 'NONE',  ( 0.3543493200069162685, -0.000000000000000000, -0.9351131265310288487 ) ) ;
#40789=CARTESIAN_POINT ( 'NONE',  ( 9.489213562373095101, -27.52281430457062328, 5.000000000000000000 ) ) ;
#40790=VERTEX_POINT ( 'NONE', #18507 ) ;
#40791=ORIENTED_EDGE ( 'NONE', *, *, #12515, .T. ) ;
#40792=EDGE_LOOP ( 'NONE', ( #44125, #103540, #141093, #107394 ) ) ;
#40794=LINE ( 'NONE', #19028, #71679 ) ;
#40795=ORIENTED_EDGE ( 'NONE', *, *, #32094, .T. ) ;
#40796=CARTESIAN_POINT ( 'NONE',  ( -19.17183060077633883, 12.75929247661559174, 4.000000000000000000 ) ) ;
#40798=ADVANCED_FACE ( 'NONE', ( #97513 ), #8339, .F. ) ;
#40801=ORIENTED_EDGE ( 'NONE', *, *, #130583, .T. ) ;
#40803=CARTESIAN_POINT ( 'NONE',  ( 57.48921356237308800, -27.52281430457095368, 5.000000000000000000 ) ) ;
#40804=CARTESIAN_POINT ( 'NONE',  ( 50.99451991528749062, 28.92564299267973738, 4.000000000000000000 ) ) ;
#40805=LINE ( 'NONE', #28510, #47216 ) ;
#40806=ORIENTED_EDGE ( 'NONE', *, *, #45502, .T. ) ;
#40807=CARTESIAN_POINT ( 'NONE',  ( 0.000000000000000000, 0.000000000000000000, 5.000000000000000000 ) ) ;
#40808=ORIENTED_EDGE ( 'NONE', *, *, #69073, .F. ) ;
#40809=DIRECTION ( 'NONE',  ( -0.7071067811865487940, 0.7071067811865463515, 0.000000000000000000 ) ) ;
#40810=CARTESIAN_POINT ( 'NONE',  ( 0.2997448713915885632, -27.71228299555206220, 4.000000000000000000 ) ) ;
#40811=CARTESIAN_POINT ( 'NONE',  ( -11.38161509397997051, -2.240707523384260824, 13.37739548510242038 ) ) ;
#40812=ORIENTED_EDGE ( 'NONE', *, *, #2759, .T. ) ;
#40813=CARTESIAN_POINT ( 'NONE',  ( 14.99999999999990763, -3.412538124160717778, 4.000000000000000000 ) ) ;
#40814=CARTESIAN_POINT ( 'NONE',  ( 30.43680103220810551, -12.74070752338415602, 9.898150129686305476 ) ) ;
#40815=DIRECTION ( 'NONE',  ( -0.7071067811865486830, -0.7071067811865464625, 0.000000000000000000 ) ) ;
#40816=VECTOR ( 'NONE', #70657, 1000.000000000000000 ) ;
#40818=PLANE ( 'NONE',  #108686 ) ;
#40819=LINE ( 'NONE', #127093, #47027 ) ;
#40820=DIRECTION ( 'NONE',  ( -0.7071067811865487940, 0.7071067811865463515, 0.000000000000000000 ) ) ;
#40821=PLANE ( 'NONE',  #132886 ) ;
#40822=FACE_OUTER_BOUND ( 'NONE', #57812, .T. ) ;
#40823=ORIENTED_EDGE ( 'NONE', *, *, #87413, .T. ) ;
#40824=ORIENTED_EDGE ( 'NONE', *, *, #30583, .T. ) ;
#40825=CARTESIAN_POINT ( 'NONE',  ( 18.48921356237309510, -27.52281430457068367, 5.000000000000000000 ) ) ;
#40826=DIRECTION ( 'NONE',  ( -0.7071067811865486830, -0.7071067811865464625, 0.000000000000000000 ) ) ;
#40828=AXIS2_PLACEMENT_3D ( 'NONE', #12743, #123695, #34517 ) ;
#40829=DIRECTION ( 'NONE',  ( -0.000000000000000000, 0.000000000000000000, 1.000000000000000000 ) ) ;
#40830=DIRECTION ( 'NONE',  ( 0.7071067811865487940, 0.7071067811865463515, 0.000000000000000000 ) ) ;
#40831=CARTESIAN_POINT ( 'NONE',  ( -0.4892135623730947680, -27.52281430457055578, 5.000000000000000000 ) ) ;
#40833=ORIENTED_EDGE ( 'NONE', *, *, #91310, .F. ) ;
#40834=DIRECTION ( 'NONE',  ( -0.6830127018922181881, 0.6830127018922202975, -0.2588190451025214056 ) ) ;
#40835=LINE ( 'NONE', #131417, #23602 ) ;
#40836=DIRECTION ( 'NONE',  ( 0.7071067811865487940, 0.7071067811865463515, 0.000000000000000000 ) ) ;
#40837=FACE_OUTER_BOUND ( 'NONE', #101665, .T. ) ;
#40839=FACE_OUTER_BOUND ( 'NONE', #36405, .T. ) ;
#40840=ORIENTED_EDGE ( 'NONE', *, *, #65609, .T. ) ;
#40844=EDGE_LOOP ( 'NONE', ( #97049, #42340, #74450, #132582 ) ) ;
#40845=LINE ( 'NONE', #73484, #8375 ) ;
#40846=CARTESIAN_POINT ( 'NONE',  ( -11.99451991528749417, 28.92564299267946382, 4.000000000000000000 ) ) ;
#40847=LINE ( 'NONE', #127881, #25230 ) ;
#40848=DIRECTION ( 'NONE',  ( 0.7071067811865487940, 0.7071067811865463515, 0.000000000000000000 ) ) ;
#40849=EDGE_CURVE ( 'NONE', #82150, #132831, #29408, .T. ) ;
#40850=CARTESIAN_POINT ( 'NONE',  ( -34.92500000000001137, 22.22500000000000142, 4.000000000000000000 ) ) ;
#40854=EDGE_CURVE ( 'NONE', #84071, #116753, #95383, .T. ) ;
#40856=ORIENTED_EDGE ( 'NONE', *, *, #134066, .T. ) ;
#40857=CARTESIAN_POINT ( 'NONE',  ( 34.49999999999975842, -2.945670655169024155, 4.994342998332159667 ) ) ;
#40858=CARTESIAN_POINT ( 'NONE',  ( 30.48921356237309510, -27.52281430457076894, 5.000000000000000000 ) ) ;
#40859=DIRECTION ( 'NONE',  ( -0.6830127018922180770, -0.6830127018922204085, -0.2588190451025213501 ) ) ;
#40860=CARTESIAN_POINT ( 'NONE',  ( -0.2997448713915885632, -27.71228299555206220, 4.000000000000000000 ) ) ;
#40861=DIRECTION ( 'NONE',  ( -0.6830127018922180770, -0.6830127018922204085, -0.2588190451025213501 ) ) ;
#40863=DIRECTION ( 'NONE',  ( 1.000000000000000000, 0.000000000000000000, 0.000000000000000000 ) ) ;
#40865=EDGE_CURVE ( 'NONE', #65878, #8725, #17800, .T. ) ;
#40867=EDGE_CURVE ( 'NONE', #131518, #77993, #106967, .T. ) ;
#40868=VECTOR ( 'NONE', #115200, 1000.000000000000227 ) ;
#40869=DIRECTION ( 'NONE',  ( 0.7071067811865486830, -0.7071067811865464625, -0.000000000000000000 ) ) ;
#40870=ORIENTED_EDGE ( 'NONE', *, *, #124288, .T. ) ;
#40871=ORIENTED_EDGE ( 'NONE', *, *, #108769, .F. ) ;
#40873=DIRECTION ( 'NONE',  ( -0.7071067811865486830, -0.7071067811865464625, -0.000000000000000000 ) ) ;
#40874=ADVANCED_FACE ( 'NONE', ( #20669 ), #131594, .F. ) ;
#40875=LINE ( 'NONE', #29267, #4483 ) ;
#40877=LINE ( 'NONE', #129286, #34448 ) ;
#40879=DIRECTION ( 'NONE',  ( 0.6830127018922180770, -0.6830127018922204085, -0.2588190451025214056 ) ) ;
#40880=EDGE_CURVE ( 'NONE', #8478, #139534, #140324, .T. ) ;
#40882=ORIENTED_EDGE ( 'NONE', *, *, #48127, .T. ) ;
#40883=DIRECTION ( 'NONE',  ( -0.7071067811865486830, -0.7071067811865464625, 0.000000000000000000 ) ) ;
#40884=ORIENTED_EDGE ( 'NONE', *, *, #46310, .T. ) ;
#40885=ORIENTED_EDGE ( 'NONE', *, *, #138887, .F. ) ;
#40886=CARTESIAN_POINT ( 'NONE',  ( 23.29289321881330110, -12.74070752338415247, 5.000000000000000000 ) ) ;
#40887=ADVANCED_FACE ( 'NONE', ( #130176 ), #6903, .F. ) ;
#40889=DIRECTION ( 'NONE',  ( -0.7071067811865487940, 0.7071067811865463515, 0.000000000000000000 ) ) ;
#40893=DIRECTION ( 'NONE',  ( -0.7071067811865487940, 0.7071067811865463515, 0.000000000000000000 ) ) ;
#40895=LINE ( 'NONE', #129308, #16089 ) ;
#40896=DIRECTION ( 'NONE',  ( 0.7071067811865487940, 0.7071067811865463515, 0.000000000000000000 ) ) ;
#40898=EDGE_CURVE ( 'NONE', #101043, #129287, #76518, .T. ) ;
#40899=LINE ( 'NONE', #74243, #9005 ) ;
#40900=VERTEX_POINT ( 'NONE', #96766 ) ;
#40902=PLANE ( 'NONE',  #50051 ) ;
#40904=CARTESIAN_POINT ( 'NONE',  ( 22.58990935480154150, 9.759292476615614831, 11.28811694763784068 ) ) ;
#40905=EDGE_CURVE ( 'NONE', #117114, #17080, #62072, .T. ) ;
#40906=PLANE ( 'NONE',  #73263 ) ;
#40907=LINE ( 'NONE', #52478, #6133 ) ;
#40908=ORIENTED_EDGE ( 'NONE', *, *, #19568, .T. ) ;
#40909=VERTEX_POINT ( 'NONE', #31570 ) ;
#40910=VECTOR ( 'NONE', #121104, 1000.000000000000000 ) ;
#40911=LINE ( 'NONE', #127934, #49179 ) ;
#40913=ORIENTED_EDGE ( 'NONE', *, *, #103899, .F. ) ;
#40914=EDGE_CURVE ( 'NONE', #75083, #59733, #30868, .T. ) ;
#40915=ORIENTED_EDGE ( 'NONE', *, *, #35708, .T. ) ;
#40916=LINE ( 'NONE', #127939, #37453 ) ;
#40917=ORIENTED_EDGE ( 'NONE', *, *, #140432, .F. ) ;
#40918=EDGE_CURVE ( 'NONE', #53085, #83276, #119956, .T. ) ;
#40919=FACE_OUTER_BOUND ( 'NONE', #135445, .T. ) ;
#40920=LINE ( 'NONE', #9696, #45641 ) ;
#40921=VECTOR ( 'NONE', #134286, 999.9999999999998863 ) ;
#40923=PLANE ( 'NONE',  #83626 ) ;
#40924=VECTOR ( 'NONE', #128305, 1000.000000000000000 ) ;
#40925=FACE_BOUND ( 'NONE', #51450, .T. ) ;
#40926=CARTESIAN_POINT ( 'NONE',  ( -28.17183060077627843, -17.24070752338410273, 4.000000000000000000 ) ) ;
#40927=FACE_OUTER_BOUND ( 'NONE', #38118, .T. ) ;
#40928=CARTESIAN_POINT ( 'NONE',  ( -34.92500000000001137, -4.199905483972744769, 4.759050581649340472 ) ) ;
#40929=LINE ( 'NONE', #50379, #129196 ) ;
#40930=EDGE_LOOP ( 'NONE', ( #8631, #124414, #79194, #1276 ) ) ;
#40931=LINE ( 'NONE', #8255, #120412 ) ;
#40933=VECTOR ( 'NONE', #93724, 1000.000000000000000 ) ;
#40934=ORIENTED_EDGE ( 'NONE', *, *, #124207, .T. ) ;
#40937=VERTEX_POINT ( 'NONE', #109108 ) ;
#40938=VECTOR ( 'NONE', #96853, 1000.000000000000000 ) ;
#40940=CARTESIAN_POINT ( 'NONE',  ( 3.679462845988301645, -22.22500000000000142, -9.628674082947240365 ) ) ;
#40942=DIRECTION ( 'NONE',  ( 0.7071067811865487940, 0.7071067811865463515, 0.000000000000000000 ) ) ;
#40943=DIRECTION ( 'NONE',  ( 1.000000000000000000, 0.000000000000000000, 0.000000000000000000 ) ) ;
#40944=LINE ( 'NONE', #8271, #140371 ) ;
#40945=CARTESIAN_POINT ( 'NONE',  ( 16.49999999999988276, 16.18958161055404332, -11.56426086740807513 ) ) ;
#40947=CARTESIAN_POINT ( 'NONE',  ( -32.99999999999976552, -6.412538124160687580, 4.000000000000000000 ) ) ;
#40949=ORIENTED_EDGE ( 'NONE', *, *, #30590, .F. ) ;
#40950=CARTESIAN_POINT ( 'NONE',  ( -3.489213562373097322, -27.52281430457057709, 5.000000000000000000 ) ) ;
#40951=CARTESIAN_POINT ( 'NONE',  ( -3.489213562373097322, -27.52281430457057709, 5.000000000000000000 ) ) ;
#40952=EDGE_LOOP ( 'NONE', ( #125751, #127803, #77501, #32013 ) ) ;
#40953=AXIS2_PLACEMENT_3D ( 'NONE', #64990, #103283, #33790 ) ;
#40954=ORIENTED_EDGE ( 'NONE', *, *, #142945, .T. ) ;
#40957=VERTEX_POINT ( 'NONE', #112683 ) ;
#40962=EDGE_CURVE ( 'NONE', #143327, #49398, #34415, .T. ) ;
#40968=VECTOR ( 'NONE', #113615, 1000.000000000000000 ) ;
#40969=ORIENTED_EDGE ( 'NONE', *, *, #51057, .F. ) ;
#40970=FACE_OUTER_BOUND ( 'NONE', #35521, .T. ) ;
#40971=CARTESIAN_POINT ( 'NONE',  ( 54.18398860626899705, 28.73617430169825226, 5.000000000000000000 ) ) ;
#40972=PLANE ( 'NONE',  #104990 ) ;
#40973=ORIENTED_EDGE ( 'NONE', *, *, #13956, .F. ) ;
#40974=ORIENTED_EDGE ( 'NONE', *, *, #4358, .F. ) ;
#40975=EDGE_CURVE ( 'NONE', #140166, #96665, #23533, .T. ) ;
#40977=LINE ( 'NONE', #75756, #107267 ) ;
#40978=EDGE_LOOP ( 'NONE', ( #61615, #20072, #116683, #80024 ) ) ;
#40979=ADVANCED_FACE ( 'NONE', ( #56915 ), #101088, .F. ) ;
#40980=CARTESIAN_POINT ( 'NONE',  ( -31.82816939922331656, -20.24070752338406720, 4.000000000000000000 ) ) ;
#40981=ORIENTED_EDGE ( 'NONE', *, *, #17739, .T. ) ;
#40982=VERTEX_POINT ( 'NONE', #46778 ) ;
#40983=ORIENTED_EDGE ( 'NONE', *, *, #65517, .F. ) ;
#40984=CARTESIAN_POINT ( 'NONE',  ( -30.48921356237309510, -27.52281430457076894, 5.000000000000000000 ) ) ;
#40985=CARTESIAN_POINT ( 'NONE',  ( 20.20710678118641113, 12.75929247661558286, 5.000000000000000000 ) ) ;
#40986=DIRECTION ( 'NONE',  ( 0.7071067811865487940, 0.7071067811865463515, 0.000000000000000000 ) ) ;
#40987=LINE ( 'NONE', #106204, #28559 ) ;
#40988=LINE ( 'NONE', #21380, #18193 ) ;
#40990=ORIENTED_EDGE ( 'NONE', *, *, #23006, .T. ) ;
#40991=LINE ( 'NONE', #139624, #122963 ) ;
#40992=VERTEX_POINT ( 'NONE', #66351 ) ;
#40993=AXIS2_PLACEMENT_3D ( 'NONE', #48636, #92837, #7228 ) ;
#40994=LINE ( 'NONE', #85191, #19347 ) ;
#40996=VERTEX_POINT ( 'NONE', #24257 ) ;
#40997=DIRECTION ( 'NONE',  ( -0.6830127018922181881, 0.6830127018922202975, -0.2588190451025214056 ) ) ;
#40998=CARTESIAN_POINT ( 'NONE',  ( -57.18398860626899705, 28.73617430169827358, 5.000000000000000000 ) ) ;
#40999=VERTEX_POINT ( 'NONE', #68504 ) ;
#41000=ORIENTED_EDGE ( 'NONE', *, *, #86875, .T. ) ;
#41001=LINE ( 'NONE', #17109, #2343 ) ;
#41002=CARTESIAN_POINT ( 'NONE',  ( 11.53839644629422345, -9.740707523384180888, 17.74957260769613399 ) ) ;
#41003=CARTESIAN_POINT ( 'NONE',  ( -32.99451991528749062, 28.92564299267960948, 4.000000000000000000 ) ) ;
#41004=CARTESIAN_POINT ( 'NONE',  ( -34.92500000000001137, 21.72500000000000142, 5.000000000000000000 ) ) ;
#41007=FACE_OUTER_BOUND ( 'NONE', #67992, .T. ) ;
#41008=DIRECTION ( 'NONE',  ( 1.000000000000000000, -0.000000000000000000, 0.000000000000000000 ) ) ;
#41009=CARTESIAN_POINT ( 'NONE',  ( -2.994519915287485734, 28.92564299267940342, 4.000000000000000000 ) ) ;
#41011=VERTEX_POINT ( 'NONE', #90960 ) ;
#41012=CARTESIAN_POINT ( 'NONE',  ( -25.49999999999981171, 4.087461875839202285, 4.000000000000000000 ) ) ;
#41014=ORIENTED_EDGE ( 'NONE', *, *, #75742, .F. ) ;
#41015=CARTESIAN_POINT ( 'NONE',  ( -13.17183060077637968, 9.759292476615618384, 4.000000000000000000 ) ) ;
#41016=CARTESIAN_POINT ( 'NONE',  ( 51.18398860626899705, 28.73617430169823095, 5.000000000000000000 ) ) ;
#41017=VERTEX_POINT ( 'NONE', #135190 ) ;
#41018=CARTESIAN_POINT ( 'NONE',  ( -21.87485380690753090, -14.24070752338414181, 9.401115078912708256 ) ) ;
#41019=LINE ( 'NONE', #72273, #111283 ) ;
#41020=ORIENTED_EDGE ( 'NONE', *, *, #25978, .T. ) ;
#41021=CARTESIAN_POINT ( 'NONE',  ( 1.499999999999984013, -7.912538124160671593, 4.000000000000000000 ) ) ;
#41022=DIRECTION ( 'NONE',  ( 0.7071067811865486830, -0.7071067811865464625, -0.000000000000000000 ) ) ;
#41023=ADVANCED_FACE ( 'NONE', ( #13351 ), #35880, .F. ) ;
#41024=EDGE_CURVE ( 'NONE', #130004, #70502, #121414, .T. ) ;
#41025=ORIENTED_EDGE ( 'NONE', *, *, #38288, .F. ) ;
#41026=VERTEX_POINT ( 'NONE', #110519 ) ;
#41027=CARTESIAN_POINT ( 'NONE',  ( 33.29974487139158867, -27.71228299555229313, 4.000000000000000000 ) ) ;
#41031=ADVANCED_FACE ( 'NONE', ( #104659 ), #93083, .T. ) ;
#41034=VERTEX_POINT ( 'NONE', #114797 ) ;
#41035=EDGE_CURVE ( 'NONE', #125641, #99168, #113384, .T. ) ;
#41036=AXIS2_PLACEMENT_3D ( 'NONE', #47398, #92250, #136481 ) ;
#41037=CARTESIAN_POINT ( 'NONE',  ( 19.17183060077633172, -20.24070752338407786, 4.000000000000000000 ) ) ;
#41039=CARTESIAN_POINT ( 'NONE',  ( 0.000000000000000000, 0.000000000000000000, 5.000000000000000000 ) ) ;
#41040=CARTESIAN_POINT ( 'NONE',  ( -34.42500000000001137, 1.541399257802000822, 5.000000000000000000 ) ) ;
#41041=CARTESIAN_POINT ( 'NONE',  ( -23.99999999999983302, 12.83542986846995149, -1.025386466790314310 ) ) ;
#41042=EDGE_CURVE ( 'NONE', #55488, #97116, #81523, .T. ) ;
#41043=ORIENTED_EDGE ( 'NONE', *, *, #85819, .T. ) ;
#41044=LINE ( 'NONE', #118594, #32890 ) ;
#41045=ADVANCED_FACE ( 'NONE', ( #16949 ), #92338, .F. ) ;
#41046=ORIENTED_EDGE ( 'NONE', *, *, #83690, .F. ) ;
#41048=FACE_OUTER_BOUND ( 'NONE', #112889, .T. ) ;
#41049=DIRECTION ( 'NONE',  ( -0.000000000000000000, 0.000000000000000000, 1.000000000000000000 ) ) ;
#41051=CARTESIAN_POINT ( 'NONE',  ( 22.49999999999985434, -11.56887692260769285, 4.000000000000000000 ) ) ;
#41052=EDGE_CURVE ( 'NONE', #48427, #50477, #1880, .T. ) ;
#41053=PLANE ( 'NONE',  #97416 ) ;
#41055=CARTESIAN_POINT ( 'NONE',  ( 5.816011393731002066, 28.73617430169783304, 5.000000000000000000 ) ) ;
#41056=VERTEX_POINT ( 'NONE', #25670 ) ;
#41057=CARTESIAN_POINT ( 'NONE',  ( 21.18398860626899349, 28.73617430169802134, 5.000000000000000000 ) ) ;
#41058=DIRECTION ( 'NONE',  ( -0.6830127018922180770, -0.6830127018922204085, -0.2588190451025213501 ) ) ;
#41059=CARTESIAN_POINT ( 'NONE',  ( 27.70612307739175861, 22.22500000000000142, 4.000000000000000000 ) ) ;
#41060=EDGE_CURVE ( 'NONE', #47726, #59437, #48875, .T. ) ;
#41062=VECTOR ( 'NONE', #95999, 1000.000000000000000 ) ;
#41063=ORIENTED_EDGE ( 'NONE', *, *, #55929, .F. ) ;
#41064=ORIENTED_EDGE ( 'NONE', *, *, #79559, .F. ) ;
#41067=VERTEX_POINT ( 'NONE', #38009 ) ;
#41070=CARTESIAN_POINT ( 'NONE',  ( -6.707106781186491062, 8.259292476615636147, 5.000000000000000000 ) ) ;
#41071=VECTOR ( 'NONE', #14316, 1000.000000000000227 ) ;
#41072=CARTESIAN_POINT ( 'NONE',  ( 21.48921356237309155, -27.52281430457070499, 5.000000000000000000 ) ) ;
#41074=PLANE ( 'NONE',  #139432 ) ;
#41076=ORIENTED_EDGE ( 'NONE', *, *, #89242, .F. ) ;
#41077=CARTESIAN_POINT ( 'NONE',  ( -24.89279686680829329, 1.949462372756119333, 4.672399651904018292 ) ) ;
#41078=ADVANCED_FACE ( 'NONE', ( #136566 ), #102548, .T. ) ;
#41079=PLANE ( 'NONE',  #59505 ) ;
#41081=ADVANCED_FACE ( 'NONE', ( #103227 ), #82234, .F. ) ;
#41084=FACE_OUTER_BOUND ( 'NONE', #31150, .T. ) ;
#41085=DIRECTION ( 'NONE',  ( -0.000000000000000000, 0.3543493200069153248, 0.9351131265310292928 ) ) ;
#41086=DIRECTION ( 'NONE',  ( -0.000000000000000000, -0.3543493200069152693, 0.9351131265310292928 ) ) ;
#41088=VECTOR ( 'NONE', #92434, 999.9999999999998863 ) ;
#41089=DIRECTION ( 'NONE',  ( 0.7071067811865486830, -0.7071067811865464625, -0.000000000000000000 ) ) ;
#41090=EDGE_CURVE ( 'NONE', #111985, #109319, #16753, .T. ) ;
#41091=LINE ( 'NONE', #85289, #102152 ) ;
#41095=VERTEX_POINT ( 'NONE', #30697 ) ;
#41096=EDGE_LOOP ( 'NONE', ( #122406, #53713, #6296, #13693 ) ) ;
#41097=EDGE_CURVE ( 'NONE', #142771, #103184, #129990, .T. ) ;
#41098=ORIENTED_EDGE ( 'NONE', *, *, #34369, .T. ) ;
#41099=VECTOR ( 'NONE', #33093, 1000.000000000000000 ) ;
#41101=( BOUNDED_CURVE ( )  B_SPLINE_CURVE ( 3, ( #135360, #34598, #45504, #36045 ),
 .UNSPECIFIED., .F., .F. ) 
 B_SPLINE_CURVE_WITH_KNOTS ( ( 4, 4 ),
 ( 5.143245962375971203, 6.645403452391246191 ),
 .UNSPECIFIED. ) 
 CURVE ( )  GEOMETRIC_REPRESENTATION_ITEM ( )  RATIONAL_B_SPLINE_CURVE ( ( 1.000000000000000000, 0.8206354192515254997, 0.8206354192515254997, 1.000000000000000000 ) ) 
 REPRESENTATION_ITEM ( '' )  );
#41103=FACE_OUTER_BOUND ( 'NONE', #51713, .T. ) ;
#41104=ORIENTED_EDGE ( 'NONE', *, *, #139354, .T. ) ;
#41106=CARTESIAN_POINT ( 'NONE',  ( -23.99999999999982592, -6.412538124160692909, 4.000000000000000000 ) ) ;
#41107=EDGE_CURVE ( 'NONE', #30424, #135054, #84376, .T. ) ;
#41108=FACE_OUTER_BOUND ( 'NONE', #107747, .T. ) ;
#41109=LINE ( 'NONE', #104932, #73951 ) ;
#41110=CARTESIAN_POINT ( 'NONE',  ( -2.700255128608413990, -27.71228299555204089, 4.000000000000000000 ) ) ;
#41111=ORIENTED_EDGE ( 'NONE', *, *, #77957, .F. ) ;
#41112=DIRECTION ( 'NONE',  ( -0.000000000000000000, 0.3543493200069153248, 0.9351131265310292928 ) ) ;
#41113=DIRECTION ( 'NONE',  ( 0.6830127018922181881, 0.6830127018922202975, -0.2588190451025214056 ) ) ;
#41114=ORIENTED_EDGE ( 'NONE', *, *, #55260, .T. ) ;
#41115=DIRECTION ( 'NONE',  ( -1.000000000000000000, 0.000000000000000000, 0.000000000000000000 ) ) ;
#41116=EDGE_CURVE ( 'NONE', #31939, #69693, #53117, .T. ) ;
#41118=EDGE_CURVE ( 'NONE', #71286, #135278, #6725, .T. ) ;
#41119=LINE ( 'NONE', #139750, #99178 ) ;
#41122=VERTEX_POINT ( 'NONE', #64025 ) ;
#41123=ORIENTED_EDGE ( 'NONE', *, *, #19505, .F. ) ;
#41124=EDGE_CURVE ( 'NONE', #51392, #13028, #8854, .T. ) ;
#41125=DIRECTION ( 'NONE',  ( 0.7071067811865487940, 0.7071067811865463515, -0.000000000000000000 ) ) ;
#41126=VECTOR ( 'NONE', #15219, 1000.000000000000000 ) ;
#41128=DIRECTION ( 'NONE',  ( 0.7071067811865487940, 0.7071067811865463515, -0.000000000000000000 ) ) ;
#41129=CARTESIAN_POINT ( 'NONE',  ( -34.92500000000001137, 12.00612307739180551, 4.000000000000000000 ) ) ;
#41130=CARTESIAN_POINT ( 'NONE',  ( 15.06011071044010485, -9.740707523384184441, 10.89222023123377348 ) ) ;
#41131=CARTESIAN_POINT ( 'NONE',  ( 11.99999999999992006, -13.44781430457068794, 5.000000000000000000 ) ) ;
#41132=EDGE_CURVE ( 'NONE', #25784, #31384, #97320, .T. ) ;
#41133=CARTESIAN_POINT ( 'NONE',  ( 5.999999999999967137, -1.447814304570820276, 5.000000000000000000 ) ) ;
#41134=CARTESIAN_POINT ( 'NONE',  ( -2.999999999999975131, -2.904428200921311376, -6.989807076074934677 ) ) ;
#41135=EDGE_LOOP ( 'NONE', ( #35672, #84672, #131329, #34697, #65340, #120451 ) ) ;
#41136=VECTOR ( 'NONE', #69968, 1000.000000000000000 ) ;
#41137=ADVANCED_FACE ( 'NONE', ( #63343 ), #51731, .F. ) ;
#41138=DIRECTION ( 'NONE',  ( -0.7071067811865486830, 0.7071067811865464625, 0.000000000000000000 ) ) ;
#41139=ORIENTED_EDGE ( 'NONE', *, *, #43373, .T. ) ;
#41140=VERTEX_POINT ( 'NONE', #53885 ) ;
#41141=EDGE_LOOP ( 'NONE', ( #135453, #91871, #68673 ) ) ;
#41142=ORIENTED_EDGE ( 'NONE', *, *, #139290, .T. ) ;
#41145=CARTESIAN_POINT ( 'NONE',  ( 5.994519915287488843, 28.92564299267942118, 4.000000000000000000 ) ) ;
#41148=EDGE_CURVE ( 'NONE', #7978, #65537, #141588, .T. ) ;
#41151=VERTEX_POINT ( 'NONE', #29238 ) ;
#41153=LINE ( 'NONE', #117961, #42400 ) ;
#41154=FACE_OUTER_BOUND ( 'NONE', #7269, .T. ) ;
#41155=FACE_OUTER_BOUND ( 'NONE', #10580, .T. ) ;
#41156=EDGE_LOOP ( 'NONE', ( #98891, #80349, #5287, #41342 ) ) ;
#41157=ORIENTED_EDGE ( 'NONE', *, *, #124615, .F. ) ;
#41158=ORIENTED_EDGE ( 'NONE', *, *, #107384, .F. ) ;
#41160=CARTESIAN_POINT ( 'NONE',  ( -25.17694361456247876, -22.22500000000000142, 1.306097034074463314 ) ) ;
#41162=FACE_OUTER_BOUND ( 'NONE', #2515, .T. ) ;
#41164=DIRECTION ( 'NONE',  ( -0.000000000000000000, 0.000000000000000000, 1.000000000000000000 ) ) ;
#41165=CARTESIAN_POINT ( 'NONE',  ( -34.49999999999975131, -20.53675388469233809, 2.352720554255813390 ) ) ;
#41167=FACE_OUTER_BOUND ( 'NONE', #26135, .T. ) ;
#41169=ORIENTED_EDGE ( 'NONE', *, *, #45934, .F. ) ;
#41171=ADVANCED_FACE ( 'NONE', ( #117646 ), #42291, .F. ) ;
#41172=FACE_OUTER_BOUND ( 'NONE', #113495, .T. ) ;
#41173=ORIENTED_EDGE ( 'NONE', *, *, #49133, .F. ) ;
#41174=CARTESIAN_POINT ( 'NONE',  ( 7.499999999999947597, -13.91253812416061386, 4.000000000000000000 ) ) ;
#41176=ORIENTED_EDGE ( 'NONE', *, *, #68274, .T. ) ;
#41177=CARTESIAN_POINT ( 'NONE',  ( 0.4892135623730947680, -27.52281430457055578, 5.000000000000000000 ) ) ;
#41178=FACE_OUTER_BOUND ( 'NONE', #506, .T. ) ;
#41179=AXIS2_PLACEMENT_3D ( 'NONE', #71439, #60593, #64660 ) ;
#41181=DIRECTION ( 'NONE',  ( -0.6830127018922181881, 0.6830127018922202975, -0.2588190451025214056 ) ) ;
#41182=VERTEX_POINT ( 'NONE', #51010 ) ;
#41185=EDGE_CURVE ( 'NONE', #126336, #66418, #129257, .T. ) ;
#41186=DIRECTION ( 'NONE',  ( -0.000000000000000000, 0.3543493200069153248, 0.9351131265310292928 ) ) ;
#41187=DIRECTION ( 'NONE',  ( -0.000000000000000000, 0.3543493200069153248, 0.9351131265310292928 ) ) ;
#41188=ADVANCED_FACE ( 'NONE', ( #62603 ), #106788, .T. ) ;
#41189=DIRECTION ( 'NONE',  ( -0.6830127018922181881, 0.6830127018922202975, -0.2588190451025214056 ) ) ;
#41191=CARTESIAN_POINT ( 'NONE',  ( 26.99999999999980815, -0.8619312979531723595, -5.102805207349763172 ) ) ;
#41194=DIRECTION ( 'NONE',  ( -0.7071067811865486830, -0.7071067811865464625, 0.000000000000000000 ) ) ;
#41195=CARTESIAN_POINT ( 'NONE',  ( 8.207106781186489286, -17.24070752338410273, 5.000000000000000000 ) ) ;
#41196=EDGE_CURVE ( 'NONE', #58969, #63466, #61903, .T. ) ;
#41197=ORIENTED_EDGE ( 'NONE', *, *, #131826, .T. ) ;
#41198=VERTEX_POINT ( 'NONE', #52413 ) ;
#41203=LINE ( 'NONE', #20872, #75798 ) ;
#41204=LINE ( 'NONE', #130383, #115622 ) ;
#41205=CARTESIAN_POINT ( 'NONE',  ( -7.828169399223474656, -14.24070752338414181, 4.000000000000000000 ) ) ;
#41206=CARTESIAN_POINT ( 'NONE',  ( 34.49999999999976552, 21.05432934483073026, 4.994342998332161443 ) ) ;
#41207=ORIENTED_EDGE ( 'NONE', *, *, #110362, .T. ) ;
#41208=LINE ( 'NONE', #107179, #51041 ) ;
#41209=EDGE_CURVE ( 'NONE', #46033, #142592, #77067, .T. ) ;
#41211=VECTOR ( 'NONE', #76625, 1000.000000000000000 ) ;
#41212=CARTESIAN_POINT ( 'NONE',  ( -35.99451991528749772, 28.92564299267963079, 4.000000000000000000 ) ) ;
#41213=EDGE_CURVE ( 'NONE', #16399, #60444, #56760, .T. ) ;
#41215=FACE_OUTER_BOUND ( 'NONE', #95258, .T. ) ;
#41216=EDGE_LOOP ( 'NONE', ( #43434, #124541, #49751, #41922 ) ) ;
#41218=DIRECTION ( 'NONE',  ( -0.000000000000000000, -0.3543493200069152693, 0.9351131265310292928 ) ) ;
#41219=DIRECTION ( 'NONE',  ( 0.3543493200069162685, -0.000000000000000000, -0.9351131265310288487 ) ) ;
#41220=DIRECTION ( 'NONE',  ( -0.000000000000000000, 0.000000000000000000, 1.000000000000000000 ) ) ;
#41221=EDGE_CURVE ( 'NONE', #91203, #78911, #55298, .T. ) ;
#41222=LINE ( 'NONE', #30353, #58510 ) ;
#41223=ORIENTED_EDGE ( 'NONE', *, *, #80035, .T. ) ;
#41224=VERTEX_POINT ( 'NONE', #1576 ) ;
#41225=ORIENTED_EDGE ( 'NONE', *, *, #115191, .F. ) ;
#41228=ORIENTED_EDGE ( 'NONE', *, *, #71155, .F. ) ;
#41230=LINE ( 'NONE', #7876, #73256 ) ;
#41233=DIRECTION ( 'NONE',  ( 0.6830127018922180770, -0.6830127018922204085, -0.2588190451025213501 ) ) ;
#41235=ORIENTED_EDGE ( 'NONE', *, *, #123722, .F. ) ;
#41236=DIRECTION ( 'NONE',  ( 0.7071067811865487940, 0.7071067811865463515, 0.000000000000000000 ) ) ;
#41237=CARTESIAN_POINT ( 'NONE',  ( 30.27825451568554271, 8.259292476615634371, 11.78515199841157468 ) ) ;
#41238=EDGE_CURVE ( 'NONE', #19313, #26139, #134279, .T. ) ;
#41240=DIRECTION ( 'NONE',  ( 0.7071067811865486830, -0.7071067811865464625, -0.000000000000000000 ) ) ;
#41241=ORIENTED_EDGE ( 'NONE', *, *, #15823, .F. ) ;
#41242=EDGE_LOOP ( 'NONE', ( #99543, #54554, #110117, #129007 ) ) ;
#41243=VECTOR ( 'NONE', #61300, 1000.000000000000000 ) ;
#41244=ORIENTED_EDGE ( 'NONE', *, *, #16502, .F. ) ;
#41245=DIRECTION ( 'NONE',  ( -0.000000000000000000, -0.3543493200069152693, 0.9351131265310292928 ) ) ;
#41246=CARTESIAN_POINT ( 'NONE',  ( -3.489213562373097322, -27.52281430457057709, 5.000000000000000000 ) ) ;
#41248=AXIS2_PLACEMENT_3D ( 'NONE', #141129, #56861, #133669 ) ;
#41250=CARTESIAN_POINT ( 'NONE',  ( 7.553349423367771820, 2.259292476615690770, 14.86850063742352646 ) ) ;
#41251=EDGE_CURVE ( 'NONE', #56450, #37411, #66881, .T. ) ;
#41252=VERTEX_POINT ( 'NONE', #13175 ) ;
#41253=ORIENTED_EDGE ( 'NONE', *, *, #104747, .T. ) ;
#41254=DIRECTION ( 'NONE',  ( -0.6830127018922180770, -0.6830127018922204085, -0.2588190451025213501 ) ) ;
#41255=EDGE_CURVE ( 'NONE', #3251, #130838, #76330, .T. ) ;
#41256=VERTEX_POINT ( 'NONE', #87198 ) ;
#41257=VERTEX_POINT ( 'NONE', #10332 ) ;
#41259=LINE ( 'NONE', #7906, #17060 ) ;
#41260=ORIENTED_EDGE ( 'NONE', *, *, #52527, .F. ) ;
#41261=DIRECTION ( 'NONE',  ( 0.7071067811865487940, 0.7071067811865463515, -0.000000000000000000 ) ) ;
#41263=ADVANCED_FACE ( 'NONE', ( #872 ), #110347, .F. ) ;
#41265=DIRECTION ( 'NONE',  ( 0.6830127018922180770, -0.6830127018922204085, -0.2588190451025213501 ) ) ;
#41266=VECTOR ( 'NONE', #68180, 1000.000000000000000 ) ;
#41267=CARTESIAN_POINT ( 'NONE',  ( 26.48831394071551415, 6.759292476615649470, 16.35960578974463431 ) ) ;
#41268=EDGE_LOOP ( 'NONE', ( #69084, #65418, #67895, #72279 ) ) ;
#41269=VECTOR ( 'NONE', #27428, 999.9999999999998863 ) ;
#41270=CARTESIAN_POINT ( 'NONE',  ( 34.92499999999998295, 7.711264365774191276, -0.4997969837368084201 ) ) ;
#41272=DIRECTION ( 'NONE',  ( -0.6830127018922180770, 0.6830127018922202975, -0.2588190451025213501 ) ) ;
#41273=ORIENTED_EDGE ( 'NONE', *, *, #106620, .T. ) ;
#41276=EDGE_CURVE ( 'NONE', #23205, #66308, #42997, .T. ) ;
#41277=LINE ( 'NONE', #64470, #93174 ) ;
#41279=CARTESIAN_POINT ( 'NONE',  ( 20.20710678118640047, 9.759292476615618384, 5.000000000000000000 ) ) ;
#41280=ORIENTED_EDGE ( 'NONE', *, *, #123665, .T. ) ;
#41285=PLANE ( 'NONE',  #108512 ) ;
#41286=CARTESIAN_POINT ( 'NONE',  ( -31.22850677138645636, 20.25929247661551003, 7.808871592221697355 ) ) ;
#41287=CARTESIAN_POINT ( 'NONE',  ( -34.45011844616454511, -2.997695858406015379, 5.000000000000000888 ) ) ;
#41288=DIRECTION ( 'NONE',  ( -0.3543493200069162685, -0.000000000000000000, -0.9351131265310288487 ) ) ;
#41289=LINE ( 'NONE', #17400, #8849 ) ;
#41290=CARTESIAN_POINT ( 'NONE',  ( 33.48921356237309510, -27.52281430457078670, 5.000000000000000000 ) ) ;
#41291=PLANE ( 'NONE',  #137550 ) ;
#41292=AXIS2_PLACEMENT_3D ( 'NONE', #110807, #99971, #89795 ) ;
#41293=DIRECTION ( 'NONE',  ( -0.000000000000000000, -0.3543493200069152693, 0.9351131265310292928 ) ) ;
#41294=CARTESIAN_POINT ( 'NONE',  ( -26.99999999999980815, -8.151047557385094677, -8.977947279169736561 ) ) ;
#41296=CARTESIAN_POINT ( 'NONE',  ( 45.48921356237309510, -27.52281430457087197, 5.000000000000000000 ) ) ;
#41297=DIRECTION ( 'NONE',  ( 0.7071067811865487940, 0.7071067811865463515, 0.000000000000000000 ) ) ;
#41298=ORIENTED_EDGE ( 'NONE', *, *, #54480, .T. ) ;
#41299=ORIENTED_EDGE ( 'NONE', *, *, #95204, .F. ) ;
#41300=ORIENTED_EDGE ( 'NONE', *, *, #102929, .T. ) ;
#41301=ORIENTED_EDGE ( 'NONE', *, *, #139423, .F. ) ;
#41302=CARTESIAN_POINT ( 'NONE',  ( 54.18398860626899705, 28.73617430169825226, 5.000000000000000000 ) ) ;
#41303=VERTEX_POINT ( 'NONE', #104919 ) ;
#41304=ORIENTED_EDGE ( 'NONE', *, *, #118506, .F. ) ;
#41305=DIRECTION ( 'NONE',  ( -0.6830127018922180770, -0.6830127018922204085, -0.2588190451025213501 ) ) ;
#41306=EDGE_CURVE ( 'NONE', #45356, #11807, #104173, .T. ) ;
#41307=ADVANCED_FACE ( 'NONE', ( #114370 ), #60010, .F. ) ;
#41308=CARTESIAN_POINT ( 'NONE',  ( 0.000000000000000000, 0.000000000000000000, 5.000000000000000000 ) ) ;
#41310=CARTESIAN_POINT ( 'NONE',  ( 33.79289321881321939, -17.24070752338410628, 5.000000000000000000 ) ) ;
#41313=CARTESIAN_POINT ( 'NONE',  ( 0.000000000000000000, 0.000000000000000000, 5.000000000000000000 ) ) ;
#41315=ORIENTED_EDGE ( 'NONE', *, *, #143287, .F. ) ;
#41318=DIRECTION ( 'NONE',  ( 0.7071067811865486830, -0.7071067811865464625, -0.000000000000000000 ) ) ;
#41319=CARTESIAN_POINT ( 'NONE',  ( -51.48921356237309510, -27.52281430457091460, 5.000000000000000000 ) ) ;
#41320=ORIENTED_EDGE ( 'NONE', *, *, #103177, .T. ) ;
#41321=ORIENTED_EDGE ( 'NONE', *, *, #138688, .F. ) ;
#41322=LINE ( 'NONE', #86984, #45049 ) ;
#41323=ORIENTED_EDGE ( 'NONE', *, *, #74006, .T. ) ;
#41324=LINE ( 'NONE', #85536, #41653 ) ;
#41325=DIRECTION ( 'NONE',  ( -0.3543493200069162685, -0.000000000000000000, -0.9351131265310288487 ) ) ;
#41326=DIRECTION ( 'NONE',  ( 0.7071067811865487940, -0.7071067811865463515, 0.000000000000000000 ) ) ;
#41327=DIRECTION ( 'NONE',  ( 0.7071067811865487940, 0.7071067811865463515, 0.000000000000000000 ) ) ;
#41328=EDGE_CURVE ( 'NONE', #133807, #42382, #27341, .T. ) ;
#41329=ORIENTED_EDGE ( 'NONE', *, *, #41368, .T. ) ;
#41330=DIRECTION ( 'NONE',  ( 0.6830127018922181881, 0.6830127018922202975, -0.2588190451025214056 ) ) ;
#41332=DIRECTION ( 'NONE',  ( -0.000000000000000000, -0.3543493200069152693, 0.9351131265310292928 ) ) ;
#41333=ORIENTED_EDGE ( 'NONE', *, *, #2451, .F. ) ;
#41334=LINE ( 'NONE', #64529, #23503 ) ;
#41335=VECTOR ( 'NONE', #70907, 1000.000000000000000 ) ;
#41338=ORIENTED_EDGE ( 'NONE', *, *, #64941, .F. ) ;
#41341=ORIENTED_EDGE ( 'NONE', *, *, #8085, .F. ) ;
#41342=ORIENTED_EDGE ( 'NONE', *, *, #14873, .F. ) ;
#41344=DIRECTION ( 'NONE',  ( 0.7071067811865487940, 0.7071067811865463515, 0.000000000000000000 ) ) ;
#41345=DIRECTION ( 'NONE',  ( -0.6830127018922180770, -0.6830127018922204085, -0.2588190451025213501 ) ) ;
#41347=ORIENTED_EDGE ( 'NONE', *, *, #39190, .T. ) ;
#41348=CARTESIAN_POINT ( 'NONE',  ( -25.82816939922335209, 12.75929247661558996, 4.000000000000000000 ) ) ;
#41349=VECTOR ( 'NONE', #82921, 1000.000000000000000 ) ;
#41350=CARTESIAN_POINT ( 'NONE',  ( -6.299744871391586898, -27.71228299555210484, 4.000000000000000000 ) ) ;
#41351=EDGE_CURVE ( 'NONE', #122401, #6499, #5586, .T. ) ;
#41352=DIRECTION ( 'NONE',  ( 0.7071067811865486830, -0.7071067811865464625, -0.000000000000000000 ) ) ;
#41353=CARTESIAN_POINT ( 'NONE',  ( -23.20710678118638626, 12.75929247661559529, 5.000000000000000000 ) ) ;
#41354=EDGE_CURVE ( 'NONE', #43329, #116175, #70894, .T. ) ;
#41356=LINE ( 'NONE', #63159, #137021 ) ;
#41358=LINE ( 'NONE', #118186, #83615 ) ;
#41359=DIRECTION ( 'NONE',  ( 0.7071067811865487940, 0.7071067811865463515, 0.000000000000000000 ) ) ;
#41364=CARTESIAN_POINT ( 'NONE',  ( -7.499999999999940492, -14.94781430457067906, 5.000000000000000000 ) ) ;
#41366=EDGE_CURVE ( 'NONE', #9952, #85558, #81053, .T. ) ;
#41367=ORIENTED_EDGE ( 'NONE', *, *, #19686, .T. ) ;
#41368=EDGE_CURVE ( 'NONE', #17308, #86287, #15041, .T. ) ;
#41369=EDGE_LOOP ( 'NONE', ( #22495, #10116, #79319, #128449 ) ) ;
#41370=VERTEX_POINT ( 'NONE', #25944 ) ;
#41374=EDGE_LOOP ( 'NONE', ( #132619, #870, #67578, #22200 ) ) ;
#41375=VERTEX_POINT ( 'NONE', #138272 ) ;
#41376=CARTESIAN_POINT ( 'NONE',  ( 26.99999999999981171, -7.068876922607739921, 4.000000000000000000 ) ) ;
#41377=DIRECTION ( 'NONE',  ( -0.000000000000000000, 0.000000000000000000, 1.000000000000000000 ) ) ;
#41378=ORIENTED_EDGE ( 'NONE', *, *, #98797, .F. ) ;
#41379=AXIS2_PLACEMENT_3D ( 'NONE', #100251, #56791, #173 ) ;
#41380=DIRECTION ( 'NONE',  ( -0.000000000000000000, -0.3543493200069152693, 0.9351131265310292928 ) ) ;
#41381=AXIS2_PLACEMENT_3D ( 'NONE', #129446, #107688, #83847 ) ;
#41382=DIRECTION ( 'NONE',  ( -0.000000000000000000, 0.3543493200069153248, 0.9351131265310292928 ) ) ;
#41383=VECTOR ( 'NONE', #32285, 1000.000000000000000 ) ;
#41384=ADVANCED_FACE ( 'NONE', ( #116516 ), #83925, .F. ) ;
#41385=CARTESIAN_POINT ( 'NONE',  ( -22.49999999999984013, -14.70932175296478839, -11.46312253303831774 ) ) ;
#41386=LINE ( 'NONE', #9442, #51271 ) ;
#41388=ORIENTED_EDGE ( 'NONE', *, *, #120840, .F. ) ;
#41389=ADVANCED_FACE ( 'NONE', ( #93334 ), #39692, .F. ) ;
#41392=CARTESIAN_POINT ( 'NONE',  ( 24.34427593291135139, 5.931737808750704666, 4.000000000000000000 ) ) ;
#41393=PLANE ( 'NONE',  #134901 ) ;
#41396=CARTESIAN_POINT ( 'NONE',  ( 26.11162361894743000, 9.759292476615625489, 17.35367589129206678 ) ) ;
#41397=EDGE_CURVE ( 'NONE', #140087, #55935, #82469, .T. ) ;
#41398=DIRECTION ( 'NONE',  ( 0.6830127018922180770, -0.6830127018922204085, -0.2588190451025213501 ) ) ;
#41399=ORIENTED_EDGE ( 'NONE', *, *, #57734, .F. ) ;
#41400=ORIENTED_EDGE ( 'NONE', *, *, #43, .T. ) ;
#41402=ORIENTED_EDGE ( 'NONE', *, *, #119297, .T. ) ;
#41404=CARTESIAN_POINT ( 'NONE',  ( -7.171830600776425868, 0.7592924766157104211, 4.000000000000000000 ) ) ;
#41405=EDGE_CURVE ( 'NONE', #51683, #22300, #4113, .T. ) ;
#41406=VECTOR ( 'NONE', #143148, 1000.000000000000000 ) ;
#41408=DIRECTION ( 'NONE',  ( -0.000000000000000000, -0.3543493200069152693, 0.9351131265310292928 ) ) ;
#41409=CARTESIAN_POINT ( 'NONE',  ( -51.18398860626899705, 28.73617430169823095, 5.000000000000000000 ) ) ;
#41413=VERTEX_POINT ( 'NONE', #94036 ) ;
#41414=CARTESIAN_POINT ( 'NONE',  ( 4.499999999999970690, -10.91253812416064939, 4.000000000000000000 ) ) ;
#41415=ORIENTED_EDGE ( 'NONE', *, *, #65702, .F. ) ;
#41416=EDGE_CURVE ( 'NONE', #89832, #114032, #17202, .T. ) ;
#41418=LINE ( 'NONE', #85626, #110267 ) ;
#41420=CARTESIAN_POINT ( 'NONE',  ( 24.18398860626899705, 28.73617430169804265, 5.000000000000000000 ) ) ;
#41421=ORIENTED_EDGE ( 'NONE', *, *, #48825, .F. ) ;
#41423=VERTEX_POINT ( 'NONE', #83178 ) ;
#41424=CARTESIAN_POINT ( 'NONE',  ( -24.32816939922335209, -21.74070752338406365, 4.000000000000000000 ) ) ;
#41425=DIRECTION ( 'NONE',  ( -0.6830127018922180770, -0.6830127018922204085, -0.2588190451025213501 ) ) ;
#41426=CARTESIAN_POINT ( 'NONE',  ( 11.22995720542198406, 21.73644205237998150, 5.000000000000000888 ) ) ;
#41427=EDGE_CURVE ( 'NONE', #81813, #22881, #125980, .T. ) ;
#41428=CARTESIAN_POINT ( 'NONE',  ( 12.60486233187513960, 21.75929247661549937, 21.32995629748183930 ) ) ;
#41431=ORIENTED_EDGE ( 'NONE', *, *, #133427, .T. ) ;
#41432=CARTESIAN_POINT ( 'NONE',  ( 34.45011844616451668, -4.483719188362457864, 5.000000000000000888 ) ) ;
#41433=ORIENTED_EDGE ( 'NONE', *, *, #1868, .F. ) ;
#41434=EDGE_LOOP ( 'NONE', ( #102970, #17259, #52186, #85557 ) ) ;
#41436=FACE_OUTER_BOUND ( 'NONE', #55734, .T. ) ;
#41437=EDGE_LOOP ( 'NONE', ( #139457, #19023, #79542, #67284 ) ) ;
#41438=DIRECTION ( 'NONE',  ( -0.7071067811865487940, 0.7071067811865463515, 0.000000000000000000 ) ) ;
#41439=CARTESIAN_POINT ( 'NONE',  ( 17.99451991528748351, 28.92564299267950645, 4.000000000000000000 ) ) ;
#41440=VECTOR ( 'NONE', #101189, 1000.000000000000227 ) ;
#41442=VECTOR ( 'NONE', #64981, 999.9999999999998863 ) ;
#41444=FACE_BOUND ( 'NONE', #55498, .T. ) ;
#41445=ORIENTED_EDGE ( 'NONE', *, *, #85138, .F. ) ;
#41446=CARTESIAN_POINT ( 'NONE',  ( 45.48921356237309510, -27.52281430457087197, 5.000000000000000000 ) ) ;
#41450=ORIENTED_EDGE ( 'NONE', *, *, #85034, .F. ) ;
#41451=VERTEX_POINT ( 'NONE', #62149 ) ;
#41452=VECTOR ( 'NONE', #82058, 1000.000000000000000 ) ;
#41453=CARTESIAN_POINT ( 'NONE',  ( 14.99999999999989519, -19.22509904557634997, 1.855685503482213505 ) ) ;
#41454=VERTEX_POINT ( 'NONE', #136834 ) ;
#41456=ORIENTED_EDGE ( 'NONE', *, *, #95541, .T. ) ;
#41457=FACE_OUTER_BOUND ( 'NONE', #106166, .T. ) ;
#41458=DIRECTION ( 'NONE',  ( -0.000000000000000000, 0.3543493200069153248, 0.9351131265310292928 ) ) ;
#41459=ORIENTED_EDGE ( 'NONE', *, *, #3919, .T. ) ;
#41460=ADVANCED_FACE ( 'NONE', ( #50544 ), #26648, .T. ) ;
#41461=DIRECTION ( 'NONE',  ( -0.6830127018922181881, 0.6830127018922202975, -0.2588190451025214056 ) ) ;
#41462=CARTESIAN_POINT ( 'NONE',  ( -2.999999999999974243, 13.55218569542903317, 5.000000000000000000 ) ) ;
#41463=AXIS2_PLACEMENT_3D ( 'NONE', #65287, #52922, #109473 ) ;
#41464=VECTOR ( 'NONE', #16364, 999.9999999999998863 ) ;
#41465=AXIS2_PLACEMENT_3D ( 'NONE', #98792, #141612, #74210 ) ;
#41466=DIRECTION ( 'NONE',  ( 0.6830127018922181881, 0.6830127018922202975, -0.2588190451025214056 ) ) ;
#41470=CARTESIAN_POINT ( 'NONE',  ( -41.99451991528749062, 28.92564299267967343, 4.000000000000000000 ) ) ;
#41471=VERTEX_POINT ( 'NONE', #36807 ) ;
#41474=CARTESIAN_POINT ( 'NONE',  ( 5.999999999999960032, -10.44781430457072524, 5.000000000000000000 ) ) ;
#41475=CARTESIAN_POINT ( 'NONE',  ( 0.000000000000000000, 0.000000000000000000, 5.000000000000000000 ) ) ;
#41476=ORIENTED_EDGE ( 'NONE', *, *, #20375, .T. ) ;
#41477=VECTOR ( 'NONE', #67064, 1000.000000000000000 ) ;
#41478=ORIENTED_EDGE ( 'NONE', *, *, #11456, .T. ) ;
#41479=VECTOR ( 'NONE', #65827, 1000.000000000000000 ) ;
#41480=ORIENTED_EDGE ( 'NONE', *, *, #75480, .T. ) ;
#41481=DIRECTION ( 'NONE',  ( -0.7071067811865486830, -0.7071067811865464625, 0.000000000000000000 ) ) ;
#41482=CARTESIAN_POINT ( 'NONE',  ( 13.49999999999990585, -10.91253812416064228, 4.000000000000000000 ) ) ;
#41484=EDGE_CURVE ( 'NONE', #118697, #110885, #142563, .T. ) ;
#41485=DIRECTION ( 'NONE',  ( 0.7071067811865487940, 0.7071067811865463515, 0.000000000000000000 ) ) ;
#41486=ORIENTED_EDGE ( 'NONE', *, *, #44385, .F. ) ;
#41487=VECTOR ( 'NONE', #114984, 1000.000000000000000 ) ;
#41488=CARTESIAN_POINT ( 'NONE',  ( -21.00548008471250938, 28.92564299267923644, 4.000000000000000000 ) ) ;
#41492=CARTESIAN_POINT ( 'NONE',  ( 11.51078643762690490, -27.52281430457047406, 5.000000000000000000 ) ) ;
#41495=EDGE_CURVE ( 'NONE', #133266, #110313, #109198, .T. ) ;
#41496=FACE_OUTER_BOUND ( 'NONE', #123018, .T. ) ;
#41497=CARTESIAN_POINT ( 'NONE',  ( -20.99999999999984368, -3.412538124160719555, 4.000000000000000000 ) ) ;
#41498=DIRECTION ( 'NONE',  ( -0.000000000000000000, 0.3543493200069153248, 0.9351131265310292928 ) ) ;
#41500=CARTESIAN_POINT ( 'NONE',  ( -13.49999999999989875, -10.91253812416064406, 4.000000000000000000 ) ) ;
#41501=VERTEX_POINT ( 'NONE', #29485 ) ;
#41502=DIRECTION ( 'NONE',  ( -0.000000000000000000, 0.000000000000000000, 1.000000000000000000 ) ) ;
#41503=CARTESIAN_POINT ( 'NONE',  ( -8.999999999999932498, 11.96639925780213964, 5.000000000000000000 ) ) ;
#41504=CARTESIAN_POINT ( 'NONE',  ( -23.99999999999983302, -13.06887692260768041, 4.000000000000000000 ) ) ;
#41506=ORIENTED_EDGE ( 'NONE', *, *, #59762, .T. ) ;
#41507=CARTESIAN_POINT ( 'NONE',  ( -12.32816939922343735, -9.740707523384180888, 4.000000000000000000 ) ) ;
#41509=VERTEX_POINT ( 'NONE', #75184 ) ;
#41513=LINE ( 'NONE', #129234, #88900 ) ;
#41514=CARTESIAN_POINT ( 'NONE',  ( 6.489213562373093325, -27.52281430457059841, 5.000000000000000000 ) ) ;
#41515=ORIENTED_EDGE ( 'NONE', *, *, #76028, .F. ) ;
#41516=ORIENTED_EDGE ( 'NONE', *, *, #51281, .T. ) ;
#41517=LINE ( 'NONE', #64717, #81971 ) ;
#41518=DIRECTION ( 'NONE',  ( -0.3543493200069162685, -0.000000000000000000, -0.9351131265310288487 ) ) ;
#41520=CARTESIAN_POINT ( 'NONE',  ( 34.42499999999998295, 0.000000000000000000, 4.500000000000000888 ) ) ;
#41521=DIRECTION ( 'NONE',  ( 0.7071067811865487940, 0.7071067811865463515, 0.000000000000000000 ) ) ;
#41523=EDGE_CURVE ( 'NONE', #76506, #109556, #119340, .T. ) ;
#41524=LINE ( 'NONE', #76323, #106890 ) ;
#41527=DIRECTION ( 'NONE',  ( -0.000000000000000000, 0.000000000000000000, 1.000000000000000000 ) ) ;
#41528=EDGE_CURVE ( 'NONE', #50567, #142230, #65012, .T. ) ;
#41529=ADVANCED_FACE ( 'NONE', ( #87467 ), #131682, .T. ) ;
#41530=VERTEX_POINT ( 'NONE', #52674 ) ;
#41531=CARTESIAN_POINT ( 'NONE',  ( -18.70701326429291456, -21.74070752338405654, 4.999753212805221558 ) ) ;
#41532=ORIENTED_EDGE ( 'NONE', *, *, #39102, .F. ) ;
#41533=EDGE_LOOP ( 'NONE', ( #53570, #127514, #136826, #51770 ) ) ;
#41534=AXIS2_PLACEMENT_3D ( 'NONE', #123303, #135595, #102961 ) ;
#41535=DIRECTION ( 'NONE',  ( -0.000000000000000000, -0.3543493200069152693, 0.9351131265310292928 ) ) ;
#41536=CARTESIAN_POINT ( 'NONE',  ( 30.18398860626900060, 28.73617430169808173, 5.000000000000000000 ) ) ;
#41537=VECTOR ( 'NONE', #83650, 1000.000000000000000 ) ;
#41538=AXIS2_PLACEMENT_3D ( 'NONE', #87871, #140802, #85710 ) ;
#41539=EDGE_CURVE ( 'NONE', #22717, #3810, #30954, .T. ) ;
#41540=EDGE_LOOP ( 'NONE', ( #81100, #68954, #19157 ) ) ;
#41541=( BOUNDED_CURVE ( )  B_SPLINE_CURVE ( 3, ( #18983, #17543, #72714, #63251 ),
 .UNSPECIFIED., .F., .T. ) 
 B_SPLINE_CURVE_WITH_KNOTS ( ( 4, 4 ),
 ( 5.255487504216517003, 5.308805501018120765 ),
 .UNSPECIFIED. ) 
 CURVE ( )  GEOMETRIC_REPRESENTATION_ITEM ( )  RATIONAL_B_SPLINE_CURVE ( ( 1.000000000000000000, 0.9997631132982454094, 0.9997631132982454094, 1.000000000000000000 ) ) 
 REPRESENTATION_ITEM ( '' )  );
#41543=DIRECTION ( 'NONE',  ( 0.3543493200069162685, -0.000000000000000000, -0.9351131265310288487 ) ) ;
#41544=AXIS2_PLACEMENT_3D ( 'NONE', #58475, #14182, #35973 ) ;
#41545=DIRECTION ( 'NONE',  ( 1.000000000000000000, 0.000000000000000000, 0.000000000000000000 ) ) ;
#41548=DIRECTION ( 'NONE',  ( -0.7071067811865486830, -0.7071067811865464625, -0.000000000000000000 ) ) ;
#41549=ORIENTED_EDGE ( 'NONE', *, *, #44124, .F. ) ;
#41550=EDGE_CURVE ( 'NONE', #7390, #50436, #96858, .T. ) ;
#41556=CARTESIAN_POINT ( 'NONE',  ( 33.32816939922329880, -6.740707523384202204, 4.000000000000000000 ) ) ;
#41557=DIRECTION ( 'NONE',  ( -0.6830127018922181881, 0.6830127018922202975, -0.2588190451025214056 ) ) ;
#41558=DIRECTION ( 'NONE',  ( -0.000000000000000000, -0.3543493200069152693, 0.9351131265310292928 ) ) ;
#41560=EDGE_CURVE ( 'NONE', #53824, #139011, #106311, .T. ) ;
#41561=DIRECTION ( 'NONE',  ( -0.6830127018922180770, -0.6830127018922204085, -0.2588190451025213501 ) ) ;
#41563=VERTEX_POINT ( 'NONE', #140405 ) ;
#41566=EDGE_CURVE ( 'NONE', #133878, #99698, #41091, .T. ) ;
#41567=DIRECTION ( 'NONE',  ( 1.000000000000000000, 0.000000000000000000, 0.000000000000000000 ) ) ;
#41568=PLANE ( 'NONE',  #46300 ) ;
#41569=VECTOR ( 'NONE', #16383, 999.9999999999998863 ) ;
#41570=CARTESIAN_POINT ( 'NONE',  ( -30.18398860626900060, 28.73617430169808173, 5.000000000000000000 ) ) ;
#41571=ORIENTED_EDGE ( 'NONE', *, *, #95191, .T. ) ;
#41572=ADVANCED_FACE ( 'NONE', ( #130266 ), #139727, .F. ) ;
#41573=DIRECTION ( 'NONE',  ( 0.6830127018922180770, -0.6830127018922204085, -0.2588190451025213501 ) ) ;
#41574=AXIS2_PLACEMENT_3D ( 'NONE', #17841, #29449, #104133 ) ;
#41576=EDGE_LOOP ( 'NONE', ( #77682, #3301, #3043, #22730 ) ) ;
#41577=CARTESIAN_POINT ( 'NONE',  ( 5.999999999999960032, -22.06887692260759692, 4.000000000000000000 ) ) ;
#41578=ORIENTED_EDGE ( 'NONE', *, *, #134582, .F. ) ;
#41579=EDGE_LOOP ( 'NONE', ( #52313, #120015, #3754, #121730 ) ) ;
#41580=FACE_OUTER_BOUND ( 'NONE', #86540, .T. ) ;
#41581=VECTOR ( 'NONE', #71232, 1000.000000000000227 ) ;
#41582=VECTOR ( 'NONE', #24793, 1000.000000000000000 ) ;
#41584=CARTESIAN_POINT ( 'NONE',  ( 20.29289321881331531, -18.74070752338408852, 5.000000000000000000 ) ) ;
#41585=AXIS2_PLACEMENT_3D ( 'NONE', #43510, #44248, #132703 ) ;
#41586=DIRECTION ( 'NONE',  ( 0.7071067811865486830, -0.7071067811865464625, -0.000000000000000000 ) ) ;
#41587=ORIENTED_EDGE ( 'NONE', *, *, #119827, .F. ) ;
#41588=CARTESIAN_POINT ( 'NONE',  ( -23.28242261357416254, -21.73023691814493219, 5.000000000000000888 ) ) ;
#41589=FACE_OUTER_BOUND ( 'NONE', #114670, .T. ) ;
#41591=VERTEX_POINT ( 'NONE', #128810 ) ;
#41593=DIRECTION ( 'NONE',  ( -0.7071067811865486830, -0.7071067811865464625, -0.000000000000000000 ) ) ;
#41594=LINE ( 'NONE', #86553, #38479 ) ;
#41596=AXIS2_PLACEMENT_3D ( 'NONE', #37302, #138045, #26429 ) ;
#41597=ADVANCED_FACE ( 'NONE', ( #74458 ), #64277, .F. ) ;
#41598=LINE ( 'NONE', #18388, #50980 ) ;
#41599=CARTESIAN_POINT ( 'NONE',  ( -25.95484226663317173, -21.74070752338405299, 21.72585301388578571 ) ) ;
#41600=EDGE_CURVE ( 'NONE', #73177, #66788, #415, .T. ) ;
#41601=EDGE_CURVE ( 'NONE', #36869, #103933, #67891, .T. ) ;
#41606=PLANE ( 'NONE',  #134386 ) ;
#41607=CARTESIAN_POINT ( 'NONE',  ( -5.999999999999952927, 10.55218569542906160, 5.000000000000000000 ) ) ;
#41608=CARTESIAN_POINT ( 'NONE',  ( 9.793339364578407924, 21.75929247661549937, 4.998822639870711626 ) ) ;
#41610=ORIENTED_EDGE ( 'NONE', *, *, #113801, .T. ) ;
#41611=VECTOR ( 'NONE', #123236, 1000.000000000000000 ) ;
#41613=CARTESIAN_POINT ( 'NONE',  ( -24.48921356237309510, -27.52281430457072631, 5.000000000000000000 ) ) ;
#41614=ADVANCED_FACE ( 'NONE', ( #11281 ), #68581, .F. ) ;
#41615=VERTEX_POINT ( 'NONE', #123681 ) ;
#41616=ORIENTED_EDGE ( 'NONE', *, *, #10192, .F. ) ;
#41617=CARTESIAN_POINT ( 'NONE',  ( 6.083148067729274189, 21.75929247661549937, 7.311836541448064608 ) ) ;
#41618=EDGE_LOOP ( 'NONE', ( #92859, #46641, #30674, #24561 ) ) ;
#41619=CARTESIAN_POINT ( 'NONE',  ( -34.49999999999975842, -10.53574439159939757, 4.994342998332166772 ) ) ;
#41620=CARTESIAN_POINT ( 'NONE',  ( -78.18398860626899705, 28.73617430169841924, 5.000000000000000000 ) ) ;
#41621=DIRECTION ( 'NONE',  ( -0.7071067811865486830, 0.7071067811865464625, 0.000000000000000000 ) ) ;
#41622=FACE_BOUND ( 'NONE', #74905, .T. ) ;
#41623=FACE_OUTER_BOUND ( 'NONE', #41369, .T. ) ;
#41624=DIRECTION ( 'NONE',  ( -0.7071067811865486830, -0.7071067811865464625, 0.000000000000000000 ) ) ;
#41626=DIRECTION ( 'NONE',  ( 0.6830127018922181881, 0.6830127018922202975, -0.2588190451025214056 ) ) ;
#41628=CARTESIAN_POINT ( 'NONE',  ( 63.48921356237309510, -27.52281430457099631, 5.000000000000000000 ) ) ;
#41630=EDGE_LOOP ( 'NONE', ( #82070, #121218, #133405, #118126 ) ) ;
#41631=VERTEX_POINT ( 'NONE', #133818 ) ;
#41633=ORIENTED_EDGE ( 'NONE', *, *, #13608, .F. ) ;
#41634=DIRECTION ( 'NONE',  ( -0.7071067811865486830, 0.7071067811865464625, 0.000000000000000000 ) ) ;
#41635=EDGE_CURVE ( 'NONE', #104944, #118169, #78023, .T. ) ;
#41636=EDGE_CURVE ( 'NONE', #122865, #28687, #10577, .T. ) ;
#41637=ORIENTED_EDGE ( 'NONE', *, *, #60574, .F. ) ;
#41639=DIRECTION ( 'NONE',  ( -0.3543493200069163795, -9.265275131829747941E-33, -0.9351131265310288487 ) ) ;
#41640=EDGE_CURVE ( 'NONE', #57451, #141054, #112074, .T. ) ;
#41641=CARTESIAN_POINT ( 'NONE',  ( -29.54016161050242317, 18.75929247661552779, 8.305906642995418920 ) ) ;
#41642=VECTOR ( 'NONE', #25089, 1000.000000000000227 ) ;
#41643=CARTESIAN_POINT ( 'NONE',  ( -34.92500000000001137, 22.22500000000000142, 4.000000000000000000 ) ) ;
#41644=DIRECTION ( 'NONE',  ( -0.6830127018922181881, 0.6830127018922202975, -0.2588190451025214056 ) ) ;
#41646=LINE ( 'NONE', #96706, #102515 ) ;
#41647=LINE ( 'NONE', #109034, #62481 ) ;
#41648=VECTOR ( 'NONE', #132208, 1000.000000000000000 ) ;
#41649=ORIENTED_EDGE ( 'NONE', *, *, #137433, .F. ) ;
#41653=VECTOR ( 'NONE', #120285, 1000.000000000000000 ) ;
#41654=VERTEX_POINT ( 'NONE', #35245 ) ;
#41656=DIRECTION ( 'NONE',  ( 0.7071067811865487940, 0.7071067811865463515, 0.000000000000000000 ) ) ;
#41657=VECTOR ( 'NONE', #4501, 1000.000000000000000 ) ;
#41659=VERTEX_POINT ( 'NONE', #44717 ) ;
#41661=ADVANCED_FACE ( 'NONE', ( #109915 ), #2555, .T. ) ;
#41662=EDGE_LOOP ( 'NONE', ( #24320, #38319, #135181, #9593 ) ) ;
#41664=ORIENTED_EDGE ( 'NONE', *, *, #118311, .F. ) ;
#41665=VECTOR ( 'NONE', #31594, 1000.000000000000227 ) ;
#41666=DIRECTION ( 'NONE',  ( -0.000000000000000000, 0.000000000000000000, 1.000000000000000000 ) ) ;
#41667=ADVANCED_FACE ( 'NONE', ( #34501 ), #56998, .F. ) ;
#41668=EDGE_CURVE ( 'NONE', #56202, #54748, #91050, .T. ) ;
#41670=( BOUNDED_CURVE ( )  B_SPLINE_CURVE ( 3, ( #99268, #110156, #77577, #22424 ),
 .UNSPECIFIED., .F., .T. ) 
 B_SPLINE_CURVE_WITH_KNOTS ( ( 4, 4 ),
 ( 1.989451877885386466, 2.205626217416170487 ),
 .UNSPECIFIED. ) 
 CURVE ( )  GEOMETRIC_REPRESENTATION_ITEM ( )  RATIONAL_B_SPLINE_CURVE ( ( 1.000000000000000000, 0.9961095111196428542, 0.9961095111196428542, 1.000000000000000000 ) ) 
 REPRESENTATION_ITEM ( '' )  );
#41672=ORIENTED_EDGE ( 'NONE', *, *, #19404, .F. ) ;
#41673=EDGE_CURVE ( 'NONE', #72122, #108664, #23618, .T. ) ;
#41675=ORIENTED_EDGE ( 'NONE', *, *, #119384, .F. ) ;
#41676=DIRECTION ( 'NONE',  ( -0.7071067811865486830, 0.7071067811865464625, 0.000000000000000000 ) ) ;
#41677=VECTOR ( 'NONE', #92909, 1000.000000000000227 ) ;
#41678=LINE ( 'NONE', #119223, #22014 ) ;
#41679=LINE ( 'NONE', #133005, #114203 ) ;
#41680=ORIENTED_EDGE ( 'NONE', *, *, #68552, .F. ) ;
#41681=VERTEX_POINT ( 'NONE', #1131 ) ;
#41682=DIRECTION ( 'NONE',  ( 0.7071067811865486830, -0.7071067811865464625, -0.000000000000000000 ) ) ;
#41683=DIRECTION ( 'NONE',  ( -0.000000000000000000, 0.000000000000000000, 1.000000000000000000 ) ) ;
#41684=EDGE_CURVE ( 'NONE', #12168, #84409, #13427, .T. ) ;
#41686=AXIS2_PLACEMENT_3D ( 'NONE', #23579, #113429, #69991 ) ;
#41687=CARTESIAN_POINT ( 'NONE',  ( 7.031635159221873543, 2.259292476615694323, 13.77329220150639166 ) ) ;
#41688=ORIENTED_EDGE ( 'NONE', *, *, #27425, .F. ) ;
#41689=EDGE_LOOP ( 'NONE', ( #127875, #38645, #140567, #46574 ) ) ;
#41690=ORIENTED_EDGE ( 'NONE', *, *, #20282, .T. ) ;
#41691=FACE_OUTER_BOUND ( 'NONE', #54526, .T. ) ;
#41692=EDGE_CURVE ( 'NONE', #135883, #54005, #105637, .T. ) ;
#41694=DIRECTION ( 'NONE',  ( 0.000000000000000000, -1.000000000000000000, 0.000000000000000000 ) ) ;
#41695=VECTOR ( 'NONE', #46437, 1000.000000000000000 ) ;
#41696=CARTESIAN_POINT ( 'NONE',  ( 7.499999999999951150, -1.533600742197721134, 5.000000000000000000 ) ) ;
#41697=DIRECTION ( 'NONE',  ( -0.000000000000000000, -0.3543493200069152693, 0.9351131265310292928 ) ) ;
#41698=CARTESIAN_POINT ( 'NONE',  ( -26.99999999999981171, 10.21212019023806938, -2.019456568337736346 ) ) ;
#41699=DIRECTION ( 'NONE',  ( -0.000000000000000000, 0.3543493200069153248, 0.9351131265310292928 ) ) ;
#41700=EDGE_LOOP ( 'NONE', ( #75743, #1493, #110903, #130667 ) ) ;
#41701=VECTOR ( 'NONE', #113869, 999.9999999999998863 ) ;
#41703=ORIENTED_EDGE ( 'NONE', *, *, #123665, .F. ) ;
#41704=VECTOR ( 'NONE', #39287, 1000.000000000000000 ) ;
#41705=EDGE_CURVE ( 'NONE', #122015, #64534, #27903, .T. ) ;
#41706=CARTESIAN_POINT ( 'NONE',  ( -6.706792507240696644, 20.25929247661552068, 20.83292124670816392 ) ) ;
#41708=ORIENTED_EDGE ( 'NONE', *, *, #118194, .T. ) ;
#41709=AXIS2_PLACEMENT_3D ( 'NONE', #27015, #91570, #60395 ) ;
#41710=DIRECTION ( 'NONE',  ( -0.000000000000000000, 0.000000000000000000, 1.000000000000000000 ) ) ;
#41711=CARTESIAN_POINT ( 'NONE',  ( 11.99451991528749417, 28.92564299267946382, 4.000000000000000000 ) ) ;
#41712=ORIENTED_EDGE ( 'NONE', *, *, #99097, .F. ) ;
#41713=VERTEX_POINT ( 'NONE', #59836 ) ;
#41714=EDGE_CURVE ( 'NONE', #1349, #16863, #49690, .T. ) ;
#41716=CARTESIAN_POINT ( 'NONE',  ( -29.99999999999978328, -16.44781430457067373, 5.000000000000000000 ) ) ;
#41717=VECTOR ( 'NONE', #76341, 1000.000000000000000 ) ;
#41718=LINE ( 'NONE', #97503, #63235 ) ;
#41719=CARTESIAN_POINT ( 'NONE',  ( 12.70701326429294831, -21.74070752338406365, 4.999753212805217117 ) ) ;
#41723=ADVANCED_FACE ( 'NONE', ( #50383 ), #4661, .T. ) ;
#41724=DIRECTION ( 'NONE',  ( 1.000000000000000000, 0.000000000000000000, 0.000000000000000000 ) ) ;
#41725=DIRECTION ( 'NONE',  ( 0.7071067811865487940, 0.7071067811865463515, -0.000000000000000000 ) ) ;
#41726=LINE ( 'NONE', #116434, #134489 ) ;
#41727=ADVANCED_FACE ( 'NONE', ( #82305 ), #104748, .T. ) ;
#41728=ORIENTED_EDGE ( 'NONE', *, *, #138241, .F. ) ;
#41729=PLANE ( 'NONE',  #132144 ) ;
#41731=VECTOR ( 'NONE', #64687, 1000.000000000000000 ) ;
#41732=CARTESIAN_POINT ( 'NONE',  ( 10.49999999999992895, -19.53360074219753884, 5.000000000000000000 ) ) ;
#41733=CARTESIAN_POINT ( 'NONE',  ( -12.18398860626900060, 28.73617430169795739, 5.000000000000000000 ) ) ;
#41734=ORIENTED_EDGE ( 'NONE', *, *, #123751, .T. ) ;
#41736=PLANE ( 'NONE',  #103859 ) ;
#41737=DIRECTION ( 'NONE',  ( 0.7071067811865486830, -0.7071067811865464625, -0.000000000000000000 ) ) ;
#41738=ORIENTED_EDGE ( 'NONE', *, *, #17842, .T. ) ;
#41740=LINE ( 'NONE', #19271, #64938 ) ;
#41741=CARTESIAN_POINT ( 'NONE',  ( 6.792893218813409462, 12.75929247661559351, 5.000000000000000000 ) ) ;
#41742=ORIENTED_EDGE ( 'NONE', *, *, #6103, .T. ) ;
#41743=EDGE_LOOP ( 'NONE', ( #22230, #42646, #27589, #114517, #87616, #106458 ) ) ;
#41744=DIRECTION ( 'NONE',  ( 0.000000000000000000, -0.3543493200069153803, -0.9351131265310292928 ) ) ;
#41747=VECTOR ( 'NONE', #142493, 1000.000000000000000 ) ;
#41748=PLANE ( 'NONE',  #63543 ) ;
#41750=CARTESIAN_POINT ( 'NONE',  ( 30.29974487139158867, -27.71228299555227537, 4.000000000000000000 ) ) ;
#41751=LINE ( 'NONE', #98961, #18259 ) ;
#41752=ORIENTED_EDGE ( 'NONE', *, *, #94215, .F. ) ;
#41753=EDGE_CURVE ( 'NONE', #31872, #79777, #92422, .T. ) ;
#41754=CARTESIAN_POINT ( 'NONE',  ( -54.48921356237310221, -27.52281430457093236, 5.000000000000000000 ) ) ;
#41755=LINE ( 'NONE', #130206, #108722 ) ;
#41757=ORIENTED_EDGE ( 'NONE', *, *, #49253, .F. ) ;
#41758=VECTOR ( 'NONE', #133209, 1000.000000000000000 ) ;
#41759=EDGE_CURVE ( 'NONE', #83399, #126191, #138098, .T. ) ;
#41760=CARTESIAN_POINT ( 'NONE',  ( 34.49999999999975842, 15.05432934483078888, 4.994342998332163219 ) ) ;
#41762=ORIENTED_EDGE ( 'NONE', *, *, #12935, .F. ) ;
#41763=AXIS2_PLACEMENT_3D ( 'NONE', #67952, #113528, #135326 ) ;
#41765=FACE_OUTER_BOUND ( 'NONE', #8391, .T. ) ;
#41766=LINE ( 'NONE', #130939, #74897 ) ;
#41767=ORIENTED_EDGE ( 'NONE', *, *, #116058, .F. ) ;
#41768=VECTOR ( 'NONE', #7049, 1000.000000000000227 ) ;
#41769=VECTOR ( 'NONE', #99276, 1000.000000000000227 ) ;
#41771=VECTOR ( 'NONE', #18207, 1000.000000000000000 ) ;
#41772=LINE ( 'NONE', #9083, #95200 ) ;
#41773=AXIS2_PLACEMENT_3D ( 'NONE', #106351, #116553, #141145 ) ;
#41774=DIRECTION ( 'NONE',  ( 0.7071067811865487940, 0.7071067811865463515, 0.000000000000000000 ) ) ;
#41775=LINE ( 'NONE', #75144, #74084 ) ;
#41776=FACE_OUTER_BOUND ( 'NONE', #7091, .T. ) ;
#41777=LINE ( 'NONE', #50511, #15042 ) ;
#41778=ORIENTED_EDGE ( 'NONE', *, *, #70665, .T. ) ;
#41780=LINE ( 'NONE', #30174, #100868 ) ;
#41781=CARTESIAN_POINT ( 'NONE',  ( 9.299744871391588674, -27.71228299555212971, 4.000000000000000000 ) ) ;
#41782=AXIS2_PLACEMENT_3D ( 'NONE', #121787, #108041, #131990 ) ;
#41784=ORIENTED_EDGE ( 'NONE', *, *, #120508, .T. ) ;
#41785=EDGE_CURVE ( 'NONE', #59176, #118319, #137393, .T. ) ;
#41786=ORIENTED_EDGE ( 'NONE', *, *, #14943, .F. ) ;
#41789=CARTESIAN_POINT ( 'NONE',  ( 39.48921356237310221, -27.52281430457082934, 5.000000000000000000 ) ) ;
#41790=PLANE ( 'NONE',  #22543 ) ;
#41791=VECTOR ( 'NONE', #93461, 1000.000000000000227 ) ;
#41793=ORIENTED_EDGE ( 'NONE', *, *, #62675, .F. ) ;
#41794=DIRECTION ( 'NONE',  ( 0.3543493200069162685, -0.000000000000000000, -0.9351131265310288487 ) ) ;
#41795=CARTESIAN_POINT ( 'NONE',  ( -9.183988606268997046, 28.73617430169793607, 5.000000000000000000 ) ) ;
#41796=VECTOR ( 'NONE', #59318, 1000.000000000000000 ) ;
#41797=ORIENTED_EDGE ( 'NONE', *, *, #29745, .F. ) ;
#41798=VECTOR ( 'NONE', #14726, 1000.000000000000227 ) ;
#41799=LINE ( 'NONE', #141842, #95381 ) ;
#41800=VECTOR ( 'NONE', #7201, 999.9999999999998863 ) ;
#41801=CARTESIAN_POINT ( 'NONE',  ( -15.79289321881334551, -11.24070752338416845, 5.000000000000000000 ) ) ;
#41802=CARTESIAN_POINT ( 'NONE',  ( -5.816011393731002066, 28.73617430169783304, 5.000000000000000000 ) ) ;
#41805=ORIENTED_EDGE ( 'NONE', *, *, #81638, .T. ) ;
#41806=LINE ( 'NONE', #86021, #138005 ) ;
#41808=CARTESIAN_POINT ( 'NONE',  ( -12.79289321881336505, 9.759292476615616607, 5.000000000000000000 ) ) ;
#41809=LINE ( 'NONE', #86023, #46679 ) ;
#41810=DIRECTION ( 'NONE',  ( 1.000000000000000000, 0.000000000000000000, 0.000000000000000000 ) ) ;
#41811=CARTESIAN_POINT ( 'NONE',  ( -1.171830600776462061, -8.240707523384200428, 4.000000000000000000 ) ) ;
#41815=ORIENTED_EDGE ( 'NONE', *, *, #79555, .F. ) ;
#41816=VERTEX_POINT ( 'NONE', #116341 ) ;
#41817=VERTEX_POINT ( 'NONE', #36630 ) ;
#41821=CARTESIAN_POINT ( 'NONE',  ( 84.18398860626899705, 28.73617430169846187, 5.000000000000000000 ) ) ;
#41824=CARTESIAN_POINT ( 'NONE',  ( -80.99451991528748351, 28.92564299267994699, 4.000000000000000000 ) ) ;
#41829=CARTESIAN_POINT ( 'NONE',  ( 5.999999999999963585, 11.58746187583912324, 4.000000000000000000 ) ) ;
#41831=CARTESIAN_POINT ( 'NONE',  ( -7.591674519009952604, -0.7407075233842735917, 14.76736230305379038 ) ) ;
#41833=EDGE_CURVE ( 'NONE', #53085, #49793, #25033, .T. ) ;
#41834=EDGE_LOOP ( 'NONE', ( #25141, #27670, #63883, #143263 ) ) ;
#41835=LINE ( 'NONE', #73742, #62089 ) ;
#41836=ORIENTED_EDGE ( 'NONE', *, *, #53157, .T. ) ;
#41837=ORIENTED_EDGE ( 'NONE', *, *, #97429, .F. ) ;
#41838=EDGE_CURVE ( 'NONE', #41256, #46950, #106141, .T. ) ;
#41839=EDGE_CURVE ( 'NONE', #32425, #54912, #108278, .T. ) ;
#41840=ORIENTED_EDGE ( 'NONE', *, *, #63153, .T. ) ;
#41843=VERTEX_POINT ( 'NONE', #97420 ) ;
#41844=ORIENTED_EDGE ( 'NONE', *, *, #35789, .T. ) ;
#41845=VECTOR ( 'NONE', #113174, 1000.000000000000227 ) ;
#41846=ADVANCED_FACE ( 'NONE', ( #73563 ), #130816, .F. ) ;
#41847=EDGE_CURVE ( 'NONE', #45656, #73359, #64831, .T. ) ;
#41848=LINE ( 'NONE', #104948, #51225 ) ;
#41851=CARTESIAN_POINT ( 'NONE',  ( 19.49999999999986144, 9.127013188829479873, 4.802533355213541633 ) ) ;
#41852=EDGE_CURVE ( 'NONE', #2265, #67530, #140246, .T. ) ;
#41853=CARTESIAN_POINT ( 'NONE',  ( -16.22850677138654873, 20.25929247661551713, 7.808871592221731106 ) ) ;
#41854=VERTEX_POINT ( 'NONE', #63430 ) ;
#41855=CARTESIAN_POINT ( 'NONE',  ( 69.48921356237309510, -27.52281430457103895, 5.000000000000000000 ) ) ;
#41856=EDGE_CURVE ( 'NONE', #138634, #32809, #40931, .T. ) ;
#41858=DIRECTION ( 'NONE',  ( -0.7071067811865487940, 0.7071067811865463515, -0.000000000000000000 ) ) ;
#41859=DIRECTION ( 'NONE',  ( -0.7071067811865487940, 0.7071067811865463515, 0.000000000000000000 ) ) ;
#41860=AXIS2_PLACEMENT_3D ( 'NONE', #36139, #99201, #90512 ) ;
#41861=LINE ( 'NONE', #72391, #91479 ) ;
#41863=AXIS2_PLACEMENT_3D ( 'NONE', #79289, #123493, #111122 ) ;
#41864=EDGE_LOOP ( 'NONE', ( #38957, #63145, #102807, #106634 ) ) ;
#41866=ORIENTED_EDGE ( 'NONE', *, *, #405, .F. ) ;
#41867=EDGE_LOOP ( 'NONE', ( #106535, #31992, #9067, #64086 ) ) ;
#41868=EDGE_LOOP ( 'NONE', ( #107578, #13013, #23166, #102285 ) ) ;
#41870=VECTOR ( 'NONE', #16158, 1000.000000000000000 ) ;
#41874=VECTOR ( 'NONE', #61768, 1000.000000000000000 ) ;
#41875=LINE ( 'NONE', #8472, #70086 ) ;
#41876=EDGE_CURVE ( 'NONE', #21943, #25521, #140936, .T. ) ;
#41877=DIRECTION ( 'NONE',  ( -0.7071067811865487940, 0.7071067811865463515, 0.000000000000000000 ) ) ;
#41878=ORIENTED_EDGE ( 'NONE', *, *, #36114, .F. ) ;
#41880=VECTOR ( 'NONE', #81740, 999.9999999999998863 ) ;
#41881=ORIENTED_EDGE ( 'NONE', *, *, #65646, .F. ) ;
#41882=EDGE_CURVE ( 'NONE', #68883, #110486, #86589, .T. ) ;
#41884=CARTESIAN_POINT ( 'NONE',  ( 0.000000000000000000, 0.000000000000000000, 5.000000000000000000 ) ) ;
#41887=ORIENTED_EDGE ( 'NONE', *, *, #111079, .F. ) ;
#41888=EDGE_LOOP ( 'NONE', ( #29656, #139120, #15899 ) ) ;
#41889=EDGE_CURVE ( 'NONE', #99771, #29164, #75010, .T. ) ;
#41890=ORIENTED_EDGE ( 'NONE', *, *, #9758, .T. ) ;
#41891=FACE_OUTER_BOUND ( 'NONE', #72368, .T. ) ;
#41892=VECTOR ( 'NONE', #105534, 1000.000000000000000 ) ;
#41893=CARTESIAN_POINT ( 'NONE',  ( -18.48921356237309510, -27.52281430457068367, 5.000000000000000000 ) ) ;
#41894=DIRECTION ( 'NONE',  ( 0.7071067811865486830, -0.7071067811865464625, -0.000000000000000000 ) ) ;
#41895=FACE_OUTER_BOUND ( 'NONE', #42408, .T. ) ;
#41896=DIRECTION ( 'NONE',  ( 0.6830127018922180770, -0.6830127018922204085, -0.2588190451025213501 ) ) ;
#41897=AXIS2_PLACEMENT_3D ( 'NONE', #100995, #99552, #122751 ) ;
#41898=ADVANCED_FACE ( 'NONE', ( #111902 ), #132247, .F. ) ;
#41900=CARTESIAN_POINT ( 'NONE',  ( 22.82816939922337696, 18.75929247661552779, 4.000000000000000000 ) ) ;
#41902=DIRECTION ( 'NONE',  ( -0.000000000000000000, -1.000000000000000000, -0.000000000000000000 ) ) ;
#41903=CARTESIAN_POINT ( 'NONE',  ( -19.17183060077631751, -20.24070752338406365, 4.000000000000000000 ) ) ;
#41904=ADVANCED_FACE ( 'NONE', ( #55387 ), #99561, .F. ) ;
#41905=AXIS2_PLACEMENT_3D ( 'NONE', #131007, #122234, #76640 ) ;
#41906=EDGE_LOOP ( 'NONE', ( #112221, #118569, #57878, #107916 ) ) ;
#41907=CARTESIAN_POINT ( 'NONE',  ( 3.183988606268992161, 28.73617430169789699, 5.000000000000000000 ) ) ;
#41908=DIRECTION ( 'NONE',  ( 0.7071067811865487940, 0.7071067811865463515, -0.000000000000000000 ) ) ;
#41909=VECTOR ( 'NONE', #31932, 1000.000000000000000 ) ;
#41910=VERTEX_POINT ( 'NONE', #10413 ) ;
#41911=EDGE_CURVE ( 'NONE', #132567, #64833, #11110, .T. ) ;
#41912=ADVANCED_FACE ( 'NONE', ( #22698 ), #77157, .F. ) ;
#41914=CARTESIAN_POINT ( 'NONE',  ( 29.20710678118634007, 18.75929247661552424, 5.000000000000000000 ) ) ;
#41917=CARTESIAN_POINT ( 'NONE',  ( 30.79289321881325137, -14.24070752338413826, 5.000000000000000000 ) ) ;
#41918=ORIENTED_EDGE ( 'NONE', *, *, #97281, .T. ) ;
#41919=CARTESIAN_POINT ( 'NONE',  ( 20.20710678118640402, -5.240707523384230626, 5.000000000000000000 ) ) ;
#41920=ORIENTED_EDGE ( 'NONE', *, *, #79394, .F. ) ;
#41921=DIRECTION ( 'NONE',  ( -0.6830127018922180770, -0.6830127018922204085, -0.2588190451025213501 ) ) ;
#41922=ORIENTED_EDGE ( 'NONE', *, *, #37913, .T. ) ;
#41923=LINE ( 'NONE', #52076, #91462 ) ;
#41925=DIRECTION ( 'NONE',  ( 0.7071067811865487940, 0.7071067811865463515, 0.000000000000000000 ) ) ;
#41926=VECTOR ( 'NONE', #54154, 1000.000000000000000 ) ;
#41927=CARTESIAN_POINT ( 'NONE',  ( -34.25154412867554754, -11.24070752338416490, 10.39518518046017270 ) ) ;
#41928=EDGE_CURVE ( 'NONE', #139710, #131546, #78562, .T. ) ;
#41929=CARTESIAN_POINT ( 'NONE',  ( 11.67183060077639212, 20.25929247661552424, 4.000000000000000000 ) ) ;
#41930=CARTESIAN_POINT ( 'NONE',  ( 22.49999999999983302, -14.70932175296475819, -11.46312253303842432 ) ) ;
#41931=CARTESIAN_POINT ( 'NONE',  ( 31.49999999999977973, 15.43112307739202471, 4.000000000000000000 ) ) ;
#41935=PLANE ( 'NONE',  #58306 ) ;
#41936=VECTOR ( 'NONE', #39423, 1000.000000000000000 ) ;
#41938=ORIENTED_EDGE ( 'NONE', *, *, #126522, .F. ) ;
#41939=ORIENTED_EDGE ( 'NONE', *, *, #137605, .T. ) ;
#41941=ORIENTED_EDGE ( 'NONE', *, *, #122198, .T. ) ;
#41942=CARTESIAN_POINT ( 'NONE',  ( 33.47336096364195157, -5.240707523384228850, 16.25846745537503324 ) ) ;
#41943=LINE ( 'NONE', #32494, #43967 ) ;
#41947=EDGE_LOOP ( 'NONE', ( #31580, #51364, #48605, #98483 ) ) ;
#41948=CARTESIAN_POINT ( 'NONE',  ( -34.49999999999975131, 9.431123077392088661, 4.000000000000000000 ) ) ;
#41951=DIRECTION ( 'NONE',  ( -0.7071067811865486830, -0.7071067811865464625, 0.000000000000000000 ) ) ;
#41952=EDGE_LOOP ( 'NONE', ( #87528, #28787, #70562, #78280 ) ) ;
#41953=CARTESIAN_POINT ( 'NONE',  ( -34.92500000000001137, -11.24070752338416490, 4.255531930566251120 ) ) ;
#41955=VECTOR ( 'NONE', #83312, 1000.000000000000000 ) ;
#41956=CARTESIAN_POINT ( 'NONE',  ( 42.48921356237308800, -27.52281430457085065, 5.000000000000000000 ) ) ;
#41957=CARTESIAN_POINT ( 'NONE',  ( -27.70710678118634718, -0.7407075233842701500, 5.000000000000000000 ) ) ;
#41959=EDGE_LOOP ( 'NONE', ( #136274, #103984, #59909, #103960 ) ) ;
#41960=ORIENTED_EDGE ( 'NONE', *, *, #125806, .T. ) ;
#41961=ORIENTED_EDGE ( 'NONE', *, *, #133216, .F. ) ;
#41963=EDGE_LOOP ( 'NONE', ( #32057, #122124, #60336, #40990 ) ) ;
#41965=CARTESIAN_POINT ( 'NONE',  ( -27.18398860626900060, 28.73617430169806042, 5.000000000000000000 ) ) ;
#41967=VECTOR ( 'NONE', #104435, 1000.000000000000000 ) ;
#41968=LINE ( 'NONE', #87605, #14385 ) ;
#41972=AXIS2_PLACEMENT_3D ( 'NONE', #30977, #62170, #128829 ) ;
#41973=VECTOR ( 'NONE', #104169, 1000.000000000000000 ) ;
#41975=ADVANCED_FACE ( 'NONE', ( #121328 ), #45945, .F. ) ;
#41977=CARTESIAN_POINT ( 'NONE',  ( 54.48921356237310221, -27.52281430457093236, 5.000000000000000000 ) ) ;
#41978=DIRECTION ( 'NONE',  ( -0.000000000000000000, 0.000000000000000000, 1.000000000000000000 ) ) ;
#41983=AXIS2_PLACEMENT_3D ( 'NONE', #86183, #23785, #80332 ) ;
#41984=LINE ( 'NONE', #52127, #11502 ) ;
#41985=AXIS2_PLACEMENT_3D ( 'NONE', #20445, #31356, #21177 ) ;
#41986=ORIENTED_EDGE ( 'NONE', *, *, #123901, .F. ) ;
#41987=ORIENTED_EDGE ( 'NONE', *, *, #117609, .F. ) ;
#41989=DIRECTION ( 'NONE',  ( 0.6830127018922180770, -0.6830127018922204085, -0.2588190451025213501 ) ) ;
#41991=DIRECTION ( 'NONE',  ( 0.7071067811865487940, -0.7071067811865463515, 0.000000000000000000 ) ) ;
#41993=VECTOR ( 'NONE', #134503, 1000.000000000000000 ) ;
#41995=DIRECTION ( 'NONE',  ( 0.7071067811865487940, 0.7071067811865463515, 0.000000000000000000 ) ) ;
#41996=EDGE_LOOP ( 'NONE', ( #4088, #65261, #72577, #75967 ) ) ;
#41999=CARTESIAN_POINT ( 'NONE',  ( -51.29974487139158867, -27.71228299555242103, 4.000000000000000000 ) ) ;
#42000=ORIENTED_EDGE ( 'NONE', *, *, #125258, .F. ) ;
#42001=VERTEX_POINT ( 'NONE', #143091 ) ;
#42003=VECTOR ( 'NONE', #44878, 999.9999999999998863 ) ;
#42004=CARTESIAN_POINT ( 'NONE',  ( 0.7228143045705931469, -21.72500000000000142, 5.000000000000000000 ) ) ;
#42005=VERTEX_POINT ( 'NONE', #57538 ) ;
#42006=LINE ( 'NONE', #121670, #124757 ) ;
#42008=VECTOR ( 'NONE', #56701, 1000.000000000000227 ) ;
#42010=EDGE_CURVE ( 'NONE', #14592, #25060, #122027, .T. ) ;
#42011=DIRECTION ( 'NONE',  ( -0.6830127018922180770, -0.6830127018922204085, -0.2588190451025213501 ) ) ;
#42012=CARTESIAN_POINT ( 'NONE',  ( 14.99451991528749595, 28.92564299267948513, 4.000000000000000000 ) ) ;
#42013=VECTOR ( 'NONE', #135544, 1000.000000000000000 ) ;
#42014=CARTESIAN_POINT ( 'NONE',  ( -72.18398860626899705, 28.73617430169837661, 5.000000000000000000 ) ) ;
#42016=VERTEX_POINT ( 'NONE', #134374 ) ;
#42018=CARTESIAN_POINT ( 'NONE',  ( -4.499999999999967137, -17.91344420646042934, 1.358650452708453527 ) ) ;
#42019=ORIENTED_EDGE ( 'NONE', *, *, #14873, .T. ) ;
#42020=AXIS2_PLACEMENT_3D ( 'NONE', #12467, #79928, #13165 ) ;
#42022=EDGE_CURVE ( 'NONE', #79351, #20950, #35074, .T. ) ;
#42024=LINE ( 'NONE', #20225, #66734 ) ;
#42025=ORIENTED_EDGE ( 'NONE', *, *, #37781, .F. ) ;
#42026=ORIENTED_EDGE ( 'NONE', *, *, #34253, .T. ) ;
#42027=EDGE_LOOP ( 'NONE', ( #114998, #86804, #110383, #92067 ) ) ;
#42028=ADVANCED_FACE ( 'NONE', ( #111146 ), #87997, .T. ) ;
#42029=EDGE_CURVE ( 'NONE', #14374, #111466, #56122, .T. ) ;
#42031=CARTESIAN_POINT ( 'NONE',  ( 24.48921356237309510, -27.52281430457072631, 5.000000000000000000 ) ) ;
#42033=EDGE_CURVE ( 'NONE', #108474, #81238, #45245, .T. ) ;
#42035=DIRECTION ( 'NONE',  ( -0.7071067811865486830, -0.7071067811865464625, 0.000000000000000000 ) ) ;
#42036=ADVANCED_FACE ( 'NONE', ( #21317 ), #109745, .F. ) ;
#42037=LINE ( 'NONE', #28296, #126979 ) ;
#42038=LINE ( 'NONE', #129017, #71322 ) ;
#42039=VECTOR ( 'NONE', #81336, 1000.000000000000000 ) ;
#42041=DIRECTION ( 'NONE',  ( -0.3543493200069162685, -0.000000000000000000, -0.9351131265310288487 ) ) ;
#42042=DIRECTION ( 'NONE',  ( -0.3543493200069162685, -0.000000000000000000, -0.9351131265310288487 ) ) ;
#42044=DIRECTION ( 'NONE',  ( 1.000000000000000000, 0.000000000000000000, 0.000000000000000000 ) ) ;
#42046=EDGE_CURVE ( 'NONE', #57920, #16561, #71261, .T. ) ;
#42047=VERTEX_POINT ( 'NONE', #49528 ) ;
#42048=VERTEX_POINT ( 'NONE', #61140 ) ;
#42049=ORIENTED_EDGE ( 'NONE', *, *, #47497, .T. ) ;
#42050=VECTOR ( 'NONE', #77220, 1000.000000000000227 ) ;
#42051=ORIENTED_EDGE ( 'NONE', *, *, #11879, .F. ) ;
#42053=ORIENTED_EDGE ( 'NONE', *, *, #123013, .F. ) ;
#42054=ORIENTED_EDGE ( 'NONE', *, *, #13043, .F. ) ;
#42055=PLANE ( 'NONE',  #46816 ) ;
#42057=EDGE_CURVE ( 'NONE', #100907, #16046, #35797, .T. ) ;
#42058=ADVANCED_FACE ( 'NONE', ( #58281 ), #136488, .F. ) ;
#42059=CARTESIAN_POINT ( 'NONE',  ( -34.92500000000001137, 22.22500000000000142, 5.000000000000000000 ) ) ;
#42060=EDGE_LOOP ( 'NONE', ( #14190, #52325, #31437, #67413 ) ) ;
#42063=EDGE_LOOP ( 'NONE', ( #22595, #65083, #812, #123104 ) ) ;
#42064=EDGE_CURVE ( 'NONE', #42348, #92938, #90878, .T. ) ;
#42067=VERTEX_POINT ( 'NONE', #102467 ) ;
#42071=CARTESIAN_POINT ( 'NONE',  ( -27.70701326429286127, -21.74070752338406365, 4.999753212805221558 ) ) ;
#42072=ORIENTED_EDGE ( 'NONE', *, *, #2329, .T. ) ;
#42073=ORIENTED_EDGE ( 'NONE', *, *, #63865, .F. ) ;
#42074=CARTESIAN_POINT ( 'NONE',  ( -12.70710678118646264, 14.25929247661557753, 5.000000000000000000 ) ) ;
#42075=ORIENTED_EDGE ( 'NONE', *, *, #76609, .F. ) ;
#42076=CARTESIAN_POINT ( 'NONE',  ( 33.72281430457037743, -21.72499999999999432, 5.000000000000000000 ) ) ;
#42080=DIRECTION ( 'NONE',  ( -0.6830127018922180770, -0.6830127018922204085, -0.2588190451025213501 ) ) ;
#42082=ORIENTED_EDGE ( 'NONE', *, *, #48602, .F. ) ;
#42083=AXIS2_PLACEMENT_3D ( 'NONE', #116197, #69143, #60420 ) ;
#42084=CARTESIAN_POINT ( 'NONE',  ( -12.00548008471251293, 28.92564299267929684, 4.000000000000000000 ) ) ;
#42085=VECTOR ( 'NONE', #76606, 999.9999999999998863 ) ;
#42086=DIRECTION ( 'NONE',  ( 0.7071067811865487940, 0.7071067811865463515, -0.000000000000000000 ) ) ;
#42089=ORIENTED_EDGE ( 'NONE', *, *, #47697, .F. ) ;
#42091=VECTOR ( 'NONE', #131765, 1000.000000000000227 ) ;
#42094=DIRECTION ( 'NONE',  ( -0.7071067811865486830, -0.7071067811865464625, 0.000000000000000000 ) ) ;
#42096=VERTEX_POINT ( 'NONE', #105289 ) ;
#42098=ORIENTED_EDGE ( 'NONE', *, *, #30948, .F. ) ;
#42100=PLANE ( 'NONE',  #130399 ) ;
#42103=ORIENTED_EDGE ( 'NONE', *, *, #24795, .T. ) ;
#42104=FACE_OUTER_BOUND ( 'NONE', #24768, .T. ) ;
#42105=EDGE_CURVE ( 'NONE', #30015, #119678, #37923, .T. ) ;
#42106=DIRECTION ( 'NONE',  ( -0.000000000000000000, 0.3543493200069153248, 0.9351131265310292928 ) ) ;
#42107=LINE ( 'NONE', #55113, #96992 ) ;
#42108=DIRECTION ( 'NONE',  ( 0.7071067811865487940, 0.7071067811865463515, 0.000000000000000000 ) ) ;
#42109=ADVANCED_FACE ( 'NONE', ( #103832 ), #70575, .F. ) ;
#42110=PLANE ( 'NONE',  #28160 ) ;
#42112=FACE_OUTER_BOUND ( 'NONE', #127242, .T. ) ;
#42113=CARTESIAN_POINT ( 'NONE',  ( 2.994519915287485734, 28.92564299267940342, 4.000000000000000000 ) ) ;
#42114=DIRECTION ( 'NONE',  ( -0.7071067811865486830, 0.7071067811865464625, 0.000000000000000000 ) ) ;
#42115=LINE ( 'NONE', #140673, #108499 ) ;
#42116=CARTESIAN_POINT ( 'NONE',  ( -4.499999999999966249, 19.46639925780206326, 5.000000000000000000 ) ) ;
#42119=VECTOR ( 'NONE', #125995, 1000.000000000000000 ) ;
#42120=ORIENTED_EDGE ( 'NONE', *, *, #10094, .T. ) ;
#42121=ORIENTED_EDGE ( 'NONE', *, *, #104754, .F. ) ;
#42123=VERTEX_POINT ( 'NONE', #137938 ) ;
#42124=VERTEX_POINT ( 'NONE', #137224 ) ;
#42125=EDGE_CURVE ( 'NONE', #143141, #30765, #113301, .T. ) ;
#42126=VECTOR ( 'NONE', #2968, 1000.000000000000227 ) ;
#42127=EDGE_LOOP ( 'NONE', ( #55082, #118621, #113287, #1835, #13489 ) ) ;
#42128=DIRECTION ( 'NONE',  ( -0.000000000000000000, -0.3543493200069152693, 0.9351131265310292928 ) ) ;
#42129=CARTESIAN_POINT ( 'NONE',  ( -45.18398860626900415, 28.73617430169818832, 5.000000000000000000 ) ) ;
#42131=EDGE_LOOP ( 'NONE', ( #16153, #103782, #126978, #56509 ) ) ;
#42132=LINE ( 'NONE', #64571, #53266 ) ;
#42133=DIRECTION ( 'NONE',  ( -0.6830127018922180770, -0.6830127018922204085, -0.2588190451025213501 ) ) ;
#42135=CARTESIAN_POINT ( 'NONE',  ( 0.000000000000000000, 0.000000000000000000, 5.000000000000000000 ) ) ;
#42137=EDGE_CURVE ( 'NONE', #52838, #5991, #135788, .T. ) ;
#42138=ORIENTED_EDGE ( 'NONE', *, *, #27601, .T. ) ;
#42141=FACE_OUTER_BOUND ( 'NONE', #92770, .T. ) ;
#42144=CARTESIAN_POINT ( 'NONE',  ( 22.82816939922337340, -5.240707523384230626, 4.000000000000000000 ) ) ;
#42145=LINE ( 'NONE', #41396, #112281 ) ;
#42146=DIRECTION ( 'NONE',  ( -0.7071067811865487940, 0.7071067811865463515, 0.000000000000000000 ) ) ;
#42147=ORIENTED_EDGE ( 'NONE', *, *, #137017, .T. ) ;
#42148=ORIENTED_EDGE ( 'NONE', *, *, #115004, .F. ) ;
#42150=ORIENTED_EDGE ( 'NONE', *, *, #28407, .T. ) ;
#42151=CARTESIAN_POINT ( 'NONE',  ( -13.35579869995845037, 22.22500000000000142, -3.173376671670978588 ) ) ;
#42152=VECTOR ( 'NONE', #39107, 1000.000000000000227 ) ;
#42153=LINE ( 'NONE', #76932, #22339 ) ;
#42154=VECTOR ( 'NONE', #44433, 1000.000000000000000 ) ;
#42157=DIRECTION ( 'NONE',  ( 0.7071067811865486830, -0.7071067811865464625, -0.000000000000000000 ) ) ;
#42158=PLANE ( 'NONE',  #34955 ) ;
#42160=ADVANCED_FACE ( 'NONE', ( #82849 ), #4485, .T. ) ;
#42161=VERTEX_POINT ( 'NONE', #47405 ) ;
#42162=DIRECTION ( 'NONE',  ( 0.7071067811865487940, 0.7071067811865463515, 0.000000000000000000 ) ) ;
#42165=LINE ( 'NONE', #129144, #86062 ) ;
#42166=CARTESIAN_POINT ( 'NONE',  ( -66.18398860626901126, 28.73617430169833753, 5.000000000000000000 ) ) ;
#42167=VERTEX_POINT ( 'NONE', #36475 ) ;
#42169=ORIENTED_EDGE ( 'NONE', *, *, #90649, .T. ) ;
#42170=PLANE ( 'NONE',  #104964 ) ;
#42171=EDGE_CURVE ( 'NONE', #100848, #96542, #80713, .T. ) ;
#42172=LINE ( 'NONE', #31289, #25335 ) ;
#42177=ORIENTED_EDGE ( 'NONE', *, *, #8630, .T. ) ;
#42178=CARTESIAN_POINT ( 'NONE',  ( 2.994519915287485734, 28.92564299267940342, 4.000000000000000000 ) ) ;
#42179=EDGE_LOOP ( 'NONE', ( #47755, #4868, #9351, #97590 ) ) ;
#42180=VERTEX_POINT ( 'NONE', #3791 ) ;
#42181=VECTOR ( 'NONE', #66166, 999.9999999999998863 ) ;
#42182=VECTOR ( 'NONE', #41697, 1000.000000000000000 ) ;
#42183=ORIENTED_EDGE ( 'NONE', *, *, #136334, .T. ) ;
#42184=VECTOR ( 'NONE', #7162, 1000.000000000000227 ) ;
#42185=EDGE_CURVE ( 'NONE', #98878, #16866, #48075, .T. ) ;
#42186=CARTESIAN_POINT ( 'NONE',  ( 2.207106781186528810, -8.240707523384198652, 5.000000000000000000 ) ) ;
#42187=ORIENTED_EDGE ( 'NONE', *, *, #91524, .F. ) ;
#42188=DIRECTION ( 'NONE',  ( -0.000000000000000000, 0.3543493200069153248, 0.9351131265310292928 ) ) ;
#42189=VECTOR ( 'NONE', #132184, 999.9999999999998863 ) ;
#42190=VECTOR ( 'NONE', #98273, 1000.000000000000000 ) ;
#42191=VECTOR ( 'NONE', #28624, 1000.000000000000000 ) ;
#42192=CARTESIAN_POINT ( 'NONE',  ( -34.92500000000001137, -22.22500000000000142, 4.000000000000000000 ) ) ;
#42193=DIRECTION ( 'NONE',  ( 0.6830127018922181881, 0.6830127018922202975, -0.2588190451025214056 ) ) ;
#42194=FACE_BOUND ( 'NONE', #35019, .T. ) ;
#42195=EDGE_LOOP ( 'NONE', ( #113873, #88876, #4365, #108235 ) ) ;
#42196=DIRECTION ( 'NONE',  ( -0.7071067811865486830, 0.7071067811865464625, 0.000000000000000000 ) ) ;
#42197=CARTESIAN_POINT ( 'NONE',  ( -31.66020301277962190, -22.22500000000000142, 6.237153622978027556 ) ) ;
#42198=VERTEX_POINT ( 'NONE', #15392 ) ;
#42200=ORIENTED_EDGE ( 'NONE', *, *, #50259, .T. ) ;
#42201=VERTEX_POINT ( 'NONE', #92995 ) ;
#42202=FACE_OUTER_BOUND ( 'NONE', #53171, .T. ) ;
#42203=ORIENTED_EDGE ( 'NONE', *, *, #120341, .T. ) ;
#42204=EDGE_CURVE ( 'NONE', #33831, #120928, #19703, .T. ) ;
#42206=EDGE_LOOP ( 'NONE', ( #10905, #94532, #99044, #14744 ) ) ;
#42207=PLANE ( 'NONE',  #120494 ) ;
#42209=CARTESIAN_POINT ( 'NONE',  ( 48.48921356237309510, -27.52281430457089328, 5.000000000000000000 ) ) ;
#42210=ORIENTED_EDGE ( 'NONE', *, *, #20982, .F. ) ;
#42211=ADVANCED_FACE ( 'NONE', ( #63263 ), #97235, .F. ) ;
#42212=CARTESIAN_POINT ( 'NONE',  ( 63.18398860626900415, 28.73617430169831621, 5.000000000000000000 ) ) ;
#42213=CARTESIAN_POINT ( 'NONE',  ( 0.000000000000000000, 0.000000000000000000, 5.000000000000000000 ) ) ;
#42214=ADVANCED_FACE ( 'NONE', ( #62527 ), #108115, .F. ) ;
#42215=AXIS2_PLACEMENT_3D ( 'NONE', #122051, #44559, #38458 ) ;
#42220=CARTESIAN_POINT ( 'NONE',  ( 11.99999999999992717, -19.44781430457064175, 5.000000000000000000 ) ) ;
#42221=DIRECTION ( 'NONE',  ( 0.000000000000000000, 0.000000000000000000, -1.000000000000000000 ) ) ;
#42222=VERTEX_POINT ( 'NONE', #73400 ) ;
#42223=VERTEX_POINT ( 'NONE', #28468 ) ;
#42224=EDGE_LOOP ( 'NONE', ( #49672, #80623, #5438, #97425, #77802, #68324 ) ) ;
#42226=DIRECTION ( 'NONE',  ( 0.7071067811865486830, -0.7071067811865464625, -0.000000000000000000 ) ) ;
#42227=CARTESIAN_POINT ( 'NONE',  ( -31.17183060077625356, -14.24070752338413648, 4.000000000000000000 ) ) ;
#42228=EDGE_LOOP ( 'NONE', ( #37180, #103985, #54460, #42902 ) ) ;
#42230=EDGE_LOOP ( 'NONE', ( #3315, #84858, #130824, #126774 ) ) ;
#42231=PLANE ( 'NONE',  #106865 ) ;
#42232=DIRECTION ( 'NONE',  ( -0.7071067811865486830, 0.7071067811865464625, 0.000000000000000000 ) ) ;
#42233=EDGE_CURVE ( 'NONE', #143133, #57179, #72730, .T. ) ;
#42234=EDGE_CURVE ( 'NONE', #118451, #19758, #50217, .T. ) ;
#42235=CARTESIAN_POINT ( 'NONE',  ( 0.000000000000000000, 0.000000000000000000, 5.000000000000000000 ) ) ;
#42236=ORIENTED_EDGE ( 'NONE', *, *, #117786, .T. ) ;
#42237=DIRECTION ( 'NONE',  ( 1.000000000000000000, -0.000000000000000000, 0.000000000000000000 ) ) ;
#42239=EDGE_CURVE ( 'NONE', #124916, #116175, #141500, .T. ) ;
#42240=DIRECTION ( 'NONE',  ( 0.6830127018922180770, -0.6830127018922204085, -0.2588190451025213501 ) ) ;
#42243=EDGE_LOOP ( 'NONE', ( #45741, #125222, #76864, #62332 ) ) ;
#42245=DIRECTION ( 'NONE',  ( -0.7071067811865486830, -0.7071067811865464625, 0.000000000000000000 ) ) ;
#42246=AXIS2_PLACEMENT_3D ( 'NONE', #116324, #17014, #72875 ) ;
#42247=LINE ( 'NONE', #85007, #130609 ) ;
#42248=ADVANCED_FACE ( 'NONE', ( #42202 ), #140088, .F. ) ;
#42249=DIRECTION ( 'NONE',  ( -0.000000000000000000, -0.3543493200069152693, 0.9351131265310292928 ) ) ;
#42250=VERTEX_POINT ( 'NONE', #130645 ) ;
#42251=DIRECTION ( 'NONE',  ( 1.000000000000000000, 0.000000000000000000, 0.000000000000000000 ) ) ;
#42252=ORIENTED_EDGE ( 'NONE', *, *, #121714, .F. ) ;
#42253=LINE ( 'NONE', #31362, #107501 ) ;
#42255=FACE_OUTER_BOUND ( 'NONE', #133150, .T. ) ;
#42256=EDGE_LOOP ( 'NONE', ( #59570, #14217, #8769, #76568 ) ) ;
#42257=DIRECTION ( 'NONE',  ( 0.3543493200069162685, -0.000000000000000000, -0.9351131265310288487 ) ) ;
#42259=ADVANCED_FACE ( 'NONE', ( #40767 ), #127781, .F. ) ;
#42260=ORIENTED_EDGE ( 'NONE', *, *, #21727, .T. ) ;
#42263=DIRECTION ( 'NONE',  ( -0.000000000000000000, 0.3543493200069153248, 0.9351131265310292928 ) ) ;
#42264=ORIENTED_EDGE ( 'NONE', *, *, #48068, .F. ) ;
#42266=CARTESIAN_POINT ( 'NONE',  ( -20.99999999999985079, 10.93112307739207445, 4.000000000000000000 ) ) ;
#42267=EDGE_LOOP ( 'NONE', ( #13562, #97727, #133419, #43961 ) ) ;
#42268=ORIENTED_EDGE ( 'NONE', *, *, #64450, .F. ) ;
#42269=AXIS2_PLACEMENT_3D ( 'NONE', #66732, #86354, #75472 ) ;
#42271=CARTESIAN_POINT ( 'NONE',  ( -34.92500000000001137, 21.72500000000000142, 5.000000000000000000 ) ) ;
#42272=EDGE_CURVE ( 'NONE', #76593, #116708, #20402, .T. ) ;
#42275=CYLINDRICAL_SURFACE ( 'NONE', #108582, 0.5000000000000004441 ) ;
#42276=CARTESIAN_POINT ( 'NONE',  ( -34.42500000000001137, -9.022814304570477617, 5.000000000000000000 ) ) ;
#42277=VERTEX_POINT ( 'NONE', #94407 ) ;
#42279=CARTESIAN_POINT ( 'NONE',  ( -34.92500000000001137, 22.22500000000000142, 4.000000000000000000 ) ) ;
#42281=AXIS2_PLACEMENT_3D ( 'NONE', #81880, #126073, #84016 ) ;
#42282=VECTOR ( 'NONE', #129405, 1000.000000000000227 ) ;
#42283=VECTOR ( 'NONE', #58266, 1000.000000000000000 ) ;
#42284=CARTESIAN_POINT ( 'NONE',  ( 8.719980320105909399, 0.7592924766157104211, 14.27032725228010968 ) ) ;
#42286=DIRECTION ( 'NONE',  ( 0.7071067811865487940, 0.7071067811865463515, 0.000000000000000000 ) ) ;
#42288=VECTOR ( 'NONE', #42745, 1000.000000000000000 ) ;
#42289=ORIENTED_EDGE ( 'NONE', *, *, #7630, .T. ) ;
#42290=ORIENTED_EDGE ( 'NONE', *, *, #117760, .F. ) ;
#42291=PLANE ( 'NONE',  #83541 ) ;
#42293=EDGE_CURVE ( 'NONE', #74842, #117708, #29158, .T. ) ;
#42294=ORIENTED_EDGE ( 'NONE', *, *, #53156, .T. ) ;
#42295=AXIS2_PLACEMENT_3D ( 'NONE', #74049, #118236, #18948 ) ;
#42296=VECTOR ( 'NONE', #61917, 1000.000000000000000 ) ;
#42297=CARTESIAN_POINT ( 'NONE',  ( -3.888376381052390141, 9.759292476615621936, 17.35367589129214139 ) ) ;
#42298=LINE ( 'NONE', #140845, #25319 ) ;
#42300=LINE ( 'NONE', #64742, #74376 ) ;
#42301=DIRECTION ( 'NONE',  ( -0.3543493200069162685, -0.000000000000000000, -0.9351131265310288487 ) ) ;
#42302=CARTESIAN_POINT ( 'NONE',  ( -1.499999999999980460, 13.46639925780212721, 5.000000000000000000 ) ) ;
#42303=CARTESIAN_POINT ( 'NONE',  ( -11.99999999999991296, -6.033600742197678279, 5.000000000000000000 ) ) ;
#42304=EDGE_CURVE ( 'NONE', #111726, #27599, #74102, .T. ) ;
#42305=ORIENTED_EDGE ( 'NONE', *, *, #106018, .F. ) ;
#42306=PLANE ( 'NONE',  #60348 ) ;
#42307=CARTESIAN_POINT ( 'NONE',  ( 36.48921356237310221, -27.52281430457080802, 5.000000000000000000 ) ) ;
#42308=DIRECTION ( 'NONE',  ( -0.000000000000000000, 0.3543493200069153248, 0.9351131265310292928 ) ) ;
#42310=LINE ( 'NONE', #40181, #56715 ) ;
#42312=FACE_OUTER_BOUND ( 'NONE', #108508, .T. ) ;
#42315=LINE ( 'NONE', #98105, #127153 ) ;
#42317=ORIENTED_EDGE ( 'NONE', *, *, #24707, .T. ) ;
#42319=LINE ( 'NONE', #113064, #16878 ) ;
#42320=CARTESIAN_POINT ( 'NONE',  ( 1.499999999999987566, -6.839392718269127869, -8.480912228396089603 ) ) ;
#42321=PLANE ( 'NONE',  #117905 ) ;
#42323=CARTESIAN_POINT ( 'NONE',  ( -8.916851932270635217, 21.75929247661549581, 7.311836541448030857 ) ) ;
#42325=EDGE_CURVE ( 'NONE', #94991, #128697, #84971, .T. ) ;
#42326=VECTOR ( 'NONE', #141922, 999.9999999999998863 ) ;
#42327=VERTEX_POINT ( 'NONE', #116881 ) ;
#42328=DIRECTION ( 'NONE',  ( 0.7071067811865487940, -0.7071067811865463515, 0.000000000000000000 ) ) ;
#42329=VERTEX_POINT ( 'NONE', #17553 ) ;
#42332=CARTESIAN_POINT ( 'NONE',  ( -69.48921356237309510, -27.52281430457103895, 5.000000000000000000 ) ) ;
#42333=CARTESIAN_POINT ( 'NONE',  ( -51.29974487139158867, -27.71228299555242103, 4.000000000000000000 ) ) ;
#42334=PLANE ( 'NONE',  #97538 ) ;
#42335=DIRECTION ( 'NONE',  ( 0.7071067811865486830, -0.7071067811865464625, -0.000000000000000000 ) ) ;
#42336=ORIENTED_EDGE ( 'NONE', *, *, #47798, .T. ) ;
#42338=LINE ( 'NONE', #43046, #65091 ) ;
#42340=ORIENTED_EDGE ( 'NONE', *, *, #128585, .T. ) ;
#42342=EDGE_CURVE ( 'NONE', #110737, #2187, #40077, .T. ) ;
#42343=CARTESIAN_POINT ( 'NONE',  ( 12.15612307739233344, -22.22500000000000142, 4.000000000000000000 ) ) ;
#42344=CARTESIAN_POINT ( 'NONE',  ( 3.489213562373097322, -27.52281430457057709, 5.000000000000000000 ) ) ;
#42346=CARTESIAN_POINT ( 'NONE',  ( -20.99451991528748707, 28.92564299267952777, 4.000000000000000000 ) ) ;
#42347=LINE ( 'NONE', #88702, #2183 ) ;
#42348=VERTEX_POINT ( 'NONE', #129174 ) ;
#42352=PLANE ( 'NONE',  #83474 ) ;
#42353=AXIS2_PLACEMENT_3D ( 'NONE', #46126, #57009, #1140 ) ;
#42354=DIRECTION ( 'NONE',  ( -0.7071067811865487940, 0.7071067811865463515, -0.000000000000000000 ) ) ;
#42355=FACE_OUTER_BOUND ( 'NONE', #91364, .T. ) ;
#42356=ORIENTED_EDGE ( 'NONE', *, *, #1248, .F. ) ;
#42358=AXIS2_PLACEMENT_3D ( 'NONE', #125188, #80283, #4777 ) ;
#42359=CARTESIAN_POINT ( 'NONE',  ( -53.99451991528749062, 28.92564299267975869, 4.000000000000000000 ) ) ;
#42360=ORIENTED_EDGE ( 'NONE', *, *, #9284, .F. ) ;
#42361=EDGE_CURVE ( 'NONE', #56805, #108692, #51, .T. ) ;
#42362=EDGE_LOOP ( 'NONE', ( #134533, #69314, #136090, #52131 ) ) ;
#42364=ORIENTED_EDGE ( 'NONE', *, *, #69089, .T. ) ;
#42365=DIRECTION ( 'NONE',  ( 0.6830127018922180770, -0.6830127018922204085, -0.2588190451025213501 ) ) ;
#42366=CARTESIAN_POINT ( 'NONE',  ( 9.792893218813397027, -14.24070752338413648, 5.000000000000000000 ) ) ;
#42367=VECTOR ( 'NONE', #87610, 1000.000000000000000 ) ;
#42368=CARTESIAN_POINT ( 'NONE',  ( -34.42500000000001137, -15.02281430457042077, 5.000000000000000000 ) ) ;
#42369=FACE_BOUND ( 'NONE', #25276, .T. ) ;
#42370=DIRECTION ( 'NONE',  ( 0.000000000000000000, 0.000000000000000000, 1.000000000000000000 ) ) ;
#42371=CARTESIAN_POINT ( 'NONE',  ( 21.29974487139158512, -27.71228299555221142, 4.000000000000000000 ) ) ;
#42372=VECTOR ( 'NONE', #33940, 1000.000000000000000 ) ;
#42373=DIRECTION ( 'NONE',  ( 0.7071067811865487940, -0.7071067811865463515, 0.000000000000000000 ) ) ;
#42375=ORIENTED_EDGE ( 'NONE', *, *, #45403, .T. ) ;
#42378=ORIENTED_EDGE ( 'NONE', *, *, #139300, .T. ) ;
#42379=ADVANCED_FACE ( 'NONE', ( #81071 ), #87114, .F. ) ;
#42380=ORIENTED_EDGE ( 'NONE', *, *, #142809, .F. ) ;
#42382=VERTEX_POINT ( 'NONE', #57908 ) ;
#42383=DIRECTION ( 'NONE',  ( -0.000000000000000000, 0.3543493200069153248, 0.9351131265310292928 ) ) ;
#42384=DIRECTION ( 'NONE',  ( 0.7071067811865487940, -0.7071067811865463515, 0.000000000000000000 ) ) ;
#42386=VERTEX_POINT ( 'NONE', #131332 ) ;
#42387=FACE_OUTER_BOUND ( 'NONE', #99896, .T. ) ;
#42388=AXIS2_PLACEMENT_3D ( 'NONE', #37248, #14045, #80769 ) ;
#42389=EDGE_CURVE ( 'NONE', #63176, #133299, #54120, .T. ) ;
#42390=AXIS2_PLACEMENT_3D ( 'NONE', #47972, #103713, #35681 ) ;
#42391=EDGE_CURVE ( 'NONE', #46293, #1659, #21134, .T. ) ;
#42393=PLANE ( 'NONE',  #84265 ) ;
#42394=PLANE ( 'NONE',  #103925 ) ;
#42395=CARTESIAN_POINT ( 'NONE',  ( -11.18650864602353678, -15.74070752338411694, 8.904080028138968927 ) ) ;
#42396=LINE ( 'NONE', #98184, #126889 ) ;
#42397=FACE_OUTER_BOUND ( 'NONE', #81059, .T. ) ;
#42398=CARTESIAN_POINT ( 'NONE',  ( -22.49999999999983302, 19.08746187583905041, 4.000000000000000000 ) ) ;
#42399=ORIENTED_EDGE ( 'NONE', *, *, #103290, .F. ) ;
#42400=VECTOR ( 'NONE', #70955, 999.9999999999998863 ) ;
#42403=FACE_OUTER_BOUND ( 'NONE', #54813, .T. ) ;
#42404=ORIENTED_EDGE ( 'NONE', *, *, #140993, .T. ) ;
#42405=FACE_OUTER_BOUND ( 'NONE', #78886, .T. ) ;
#42406=CARTESIAN_POINT ( 'NONE',  ( -1.171830600776461617, 15.75929247661555443, 4.000000000000000000 ) ) ;
#42407=EDGE_LOOP ( 'NONE', ( #41300, #89772, #14942, #117831 ) ) ;
#42408=EDGE_LOOP ( 'NONE', ( #66180, #25062, #71220, #29971 ) ) ;
#42409=EDGE_CURVE ( 'NONE', #99416, #5794, #47749, .T. ) ;
#42411=ORIENTED_EDGE ( 'NONE', *, *, #236, .F. ) ;
#42413=ORIENTED_EDGE ( 'NONE', *, *, #63832, .F. ) ;
#42414=CARTESIAN_POINT ( 'NONE',  ( -6.005480084712508493, 28.92564299267933947, 4.000000000000000000 ) ) ;
#42415=LINE ( 'NONE', #120631, #125696 ) ;
#42416=VECTOR ( 'NONE', #79216, 1000.000000000000227 ) ;
#42419=EDGE_CURVE ( 'NONE', #74460, #3311, #136138, .T. ) ;
#42420=ORIENTED_EDGE ( 'NONE', *, *, #52586, .T. ) ;
#42421=EDGE_LOOP ( 'NONE', ( #65163, #105106, #106884, #37094 ) ) ;
#42423=CARTESIAN_POINT ( 'NONE',  ( -34.42500000000001137, -21.72500000000000142, 5.000000000000000000 ) ) ;
#42424=EDGE_CURVE ( 'NONE', #102767, #63264, #33480, .T. ) ;
#42425=LINE ( 'NONE', #31524, #130477 ) ;
#42427=VERTEX_POINT ( 'NONE', #87821 ) ;
#42429=CARTESIAN_POINT ( 'NONE',  ( -0.4892135623730947680, -27.52281430457055578, 5.000000000000000000 ) ) ;
#42430=VECTOR ( 'NONE', #58672, 1000.000000000000000 ) ;
#42431=LINE ( 'NONE', #96734, #79611 ) ;
#42432=ORIENTED_EDGE ( 'NONE', *, *, #142516, .T. ) ;
#42433=DIRECTION ( 'NONE',  ( 0.7071067811865487940, 0.7071067811865463515, 0.000000000000000000 ) ) ;
#42434=VERTEX_POINT ( 'NONE', #132063 ) ;
#42435=ORIENTED_EDGE ( 'NONE', *, *, #96256, .T. ) ;
#42436=VECTOR ( 'NONE', #142452, 999.9999999999998863 ) ;
#42437=VERTEX_POINT ( 'NONE', #77681 ) ;
#42438=CARTESIAN_POINT ( 'NONE',  ( -34.49999999999975131, -5.568876922607759461, 4.000000000000000000 ) ) ;
#42439=EDGE_CURVE ( 'NONE', #68775, #81209, #66093, .T. ) ;
#42440=CARTESIAN_POINT ( 'NONE',  ( -2.207106781186522149, 12.75929247661559351, 5.000000000000000000 ) ) ;
#42442=( BOUNDED_CURVE ( )  B_SPLINE_CURVE ( 3, ( #89602, #11292, #133833, #78743 ),
 .UNSPECIFIED., .F., .T. ) 
 B_SPLINE_CURVE_WITH_KNOTS ( ( 4, 4 ),
 ( 1.208578181583226385, 1.359146454359472678 ),
 .UNSPECIFIED. ) 
 CURVE ( )  GEOMETRIC_REPRESENTATION_ITEM ( )  RATIONAL_B_SPLINE_CURVE ( ( 1.000000000000000000, 0.9981116584018941973, 0.9981116584018941973, 1.000000000000000000 ) ) 
 REPRESENTATION_ITEM ( '' )  );
#42443=DIRECTION ( 'NONE',  ( -0.7071067811865486830, 0.7071067811865464625, 0.000000000000000000 ) ) ;
#42444=VECTOR ( 'NONE', #114093, 1000.000000000000227 ) ;
#42445=DIRECTION ( 'NONE',  ( -0.000000000000000000, -0.3543493200069152693, 0.9351131265310292928 ) ) ;
#42446=CARTESIAN_POINT ( 'NONE',  ( -27.70710678118634718, 8.259292476615637923, 5.000000000000000000 ) ) ;
#42448=PLANE ( 'NONE',  #7220 ) ;
#42451=EDGE_CURVE ( 'NONE', #135769, #104204, #102818, .T. ) ;
#42452=CARTESIAN_POINT ( 'NONE',  ( -34.49999999999975131, -19.53574439159930876, 4.994342998332169437 ) ) ;
#42453=VECTOR ( 'NONE', #37818, 1000.000000000000000 ) ;
#42454=ADVANCED_FACE ( 'NONE', ( #142232 ), #108830, .T. ) ;
#42455=DIRECTION ( 'NONE',  ( -0.7071067811865486830, -0.7071067811865464625, 0.000000000000000000 ) ) ;
#42456=VECTOR ( 'NONE', #53278, 1000.000000000000000 ) ;
#42458=DIRECTION ( 'NONE',  ( -0.000000000000000000, 0.000000000000000000, 1.000000000000000000 ) ) ;
#42459=DIRECTION ( 'NONE',  ( 0.7071067811865486830, -0.7071067811865464625, -0.000000000000000000 ) ) ;
#42460=ORIENTED_EDGE ( 'NONE', *, *, #44490, .T. ) ;
#42461=VERTEX_POINT ( 'NONE', #116534 ) ;
#42463=LINE ( 'NONE', #41002, #34954 ) ;
#42464=DIRECTION ( 'NONE',  ( 0.6830127018922180770, -0.6830127018922204085, -0.2588190451025213501 ) ) ;
#42465=VECTOR ( 'NONE', #72109, 1000.000000000000000 ) ;
#42466=CARTESIAN_POINT ( 'NONE',  ( 72.29974487139158157, -27.71228299555256669, 4.000000000000000000 ) ) ;
#42467=EDGE_CURVE ( 'NONE', #134528, #104985, #4864, .T. ) ;
#42471=DIRECTION ( 'NONE',  ( -0.7071067811865487940, 0.7071067811865463515, 0.000000000000000000 ) ) ;
#42472=LINE ( 'NONE', #76519, #122882 ) ;
#42473=ORIENTED_EDGE ( 'NONE', *, *, #30580, .F. ) ;
#42474=CARTESIAN_POINT ( 'NONE',  ( -34.49999999999975131, 7.087461875839177416, 4.000000000000000000 ) ) ;
#42476=VECTOR ( 'NONE', #116400, 1000.000000000000000 ) ;
#42477=DIRECTION ( 'NONE',  ( -0.000000000000000000, 0.000000000000000000, 1.000000000000000000 ) ) ;
#42478=ORIENTED_EDGE ( 'NONE', *, *, #98170, .F. ) ;
#42479=DIRECTION ( 'NONE',  ( -0.7071067811865487940, 0.7071067811865463515, 0.000000000000000000 ) ) ;
#42480=DIRECTION ( 'NONE',  ( -0.6830127018922180770, -0.6830127018922204085, -0.2588190451025213501 ) ) ;
#42481=EDGE_LOOP ( 'NONE', ( #77519, #139280, #125484, #75619 ) ) ;
#42482=FACE_OUTER_BOUND ( 'NONE', #18176, .T. ) ;
#42483=DIRECTION ( 'NONE',  ( -0.3543493200069162685, -0.000000000000000000, -0.9351131265310288487 ) ) ;
#42484=DIRECTION ( 'NONE',  ( 0.7071067811865487940, 0.7071067811865463515, 0.000000000000000000 ) ) ;
#42485=EDGE_LOOP ( 'NONE', ( #142236, #16434, #84280, #118538 ) ) ;
#42486=VECTOR ( 'NONE', #108411, 1000.000000000000000 ) ;
#42487=VERTEX_POINT ( 'NONE', #60776 ) ;
#42488=LINE ( 'NONE', #32305, #134325 ) ;
#42489=CARTESIAN_POINT ( 'NONE',  ( 24.70710678118637205, 8.259292476615627265, 5.000000000000000000 ) ) ;
#42491=LINE ( 'NONE', #83289, #18166 ) ;
#42493=DIRECTION ( 'NONE',  ( -0.3543493200069162685, -0.000000000000000000, -0.9351131265310288487 ) ) ;
#42494=DIRECTION ( 'NONE',  ( -0.7071067811865486830, 0.7071067811865464625, 0.000000000000000000 ) ) ;
#42495=ORIENTED_EDGE ( 'NONE', *, *, #122262, .T. ) ;
#42496=CARTESIAN_POINT ( 'NONE',  ( -31.49999999999977973, 7.466399257802189382, 5.000000000000000000 ) ) ;
#42497=ADVANCED_FACE ( 'NONE', ( #137582 ), #37563, .F. ) ;
#42498=DIRECTION ( 'NONE',  ( 0.7071067811865486830, -0.7071067811865464625, -0.000000000000000000 ) ) ;
#42500=VECTOR ( 'NONE', #118903, 1000.000000000000000 ) ;
#42502=AXIS2_PLACEMENT_3D ( 'NONE', #31331, #53811, #119722 ) ;
#42503=LINE ( 'NONE', #86708, #93086 ) ;
#42507=VECTOR ( 'NONE', #25550, 1000.000000000000000 ) ;
#42508=LINE ( 'NONE', #54108, #63221 ) ;
#42509=VERTEX_POINT ( 'NONE', #94755 ) ;
#42510=CARTESIAN_POINT ( 'NONE',  ( -27.18398860626900060, 28.73617430169806042, 5.000000000000000000 ) ) ;
#42511=CARTESIAN_POINT ( 'NONE',  ( 42.18398860626899705, 28.73617430169816700, 5.000000000000000000 ) ) ;
#42512=FACE_OUTER_BOUND ( 'NONE', #48794, .T. ) ;
#42513=EDGE_CURVE ( 'NONE', #105446, #53582, #15058, .T. ) ;
#42514=FACE_OUTER_BOUND ( 'NONE', #10919, .T. ) ;
#42515=CARTESIAN_POINT ( 'NONE',  ( 0.000000000000000000, 0.000000000000000000, 5.000000000000000000 ) ) ;
#42516=VERTEX_POINT ( 'NONE', #5602 ) ;
#42519=LINE ( 'NONE', #41781, #42486 ) ;
#42520=VECTOR ( 'NONE', #38619, 1000.000000000000227 ) ;
#42522=EDGE_CURVE ( 'NONE', #132792, #133359, #94055, .T. ) ;
#42524=VERTEX_POINT ( 'NONE', #38972 ) ;
#42526=VECTOR ( 'NONE', #83283, 1000.000000000000000 ) ;
#42527=ORIENTED_EDGE ( 'NONE', *, *, #74131, .T. ) ;
#42528=EDGE_CURVE ( 'NONE', #24434, #130179, #115064, .T. ) ;
#42531=CARTESIAN_POINT ( 'NONE',  ( -24.55388970886357569, 5.485012786255876627, 4.000000000000000000 ) ) ;
#42534=CARTESIAN_POINT ( 'NONE',  ( 20.99451991528748707, 28.92564299267952777, 4.000000000000000000 ) ) ;
#42535=DIRECTION ( 'NONE',  ( 0.7071067811865486830, -0.7071067811865464625, -0.000000000000000000 ) ) ;
#42537=EDGE_CURVE ( 'NONE', #111332, #32577, #59336, .T. ) ;
#42538=VERTEX_POINT ( 'NONE', #95482 ) ;
#42539=VECTOR ( 'NONE', #8302, 1000.000000000000000 ) ;
#42540=LINE ( 'NONE', #87455, #49047 ) ;
#42541=FACE_OUTER_BOUND ( 'NONE', #99373, .T. ) ;
#42542=DIRECTION ( 'NONE',  ( -0.7071067811865486830, 0.7071067811865464625, 0.000000000000000000 ) ) ;
#42543=ADVANCED_FACE ( 'NONE', ( #82488 ), #117216, .T. ) ;
#42544=ORIENTED_EDGE ( 'NONE', *, *, #22405, .F. ) ;
#42545=AXIS2_PLACEMENT_3D ( 'NONE', #83639, #28529, #72787 ) ;
#42546=ORIENTED_EDGE ( 'NONE', *, *, #67569, .F. ) ;
#42547=FACE_BOUND ( 'NONE', #125055, .T. ) ;
#42549=CARTESIAN_POINT ( 'NONE',  ( -28.49999999999980105, -8.947814304570739452, 5.000000000000000000 ) ) ;
#42550=LINE ( 'NONE', #413, #119969 ) ;
#42551=EDGE_CURVE ( 'NONE', #121666, #94981, #39715, .T. ) ;
#42553=AXIS2_PLACEMENT_3D ( 'NONE', #54685, #75022, #40942 ) ;
#42554=CARTESIAN_POINT ( 'NONE',  ( 31.49999999999978684, -14.70932175296474398, -11.46312253303844209 ) ) ;
#42555=EDGE_LOOP ( 'NONE', ( #86924, #47163, #135274, #47100 ) ) ;
#42556=VECTOR ( 'NONE', #83404, 999.9999999999998863 ) ;
#42557=EDGE_LOOP ( 'NONE', ( #37748, #2611, #107978, #61703 ) ) ;
#42559=ORIENTED_EDGE ( 'NONE', *, *, #67824, .F. ) ;
#42560=VERTEX_POINT ( 'NONE', #28101 ) ;
#42561=ADVANCED_FACE ( 'NONE', ( #62169 ), #16479, .F. ) ;
#42562=VECTOR ( 'NONE', #2439, 1000.000000000000227 ) ;
#42564=DIRECTION ( 'NONE',  ( -0.000000000000000000, 0.000000000000000000, 1.000000000000000000 ) ) ;
#42565=EDGE_CURVE ( 'NONE', #99104, #54925, #142919, .T. ) ;
#42567=LINE ( 'NONE', #43972, #74945 ) ;
#42568=ORIENTED_EDGE ( 'NONE', *, *, #33045, .T. ) ;
#42570=LINE ( 'NONE', #41824, #70461 ) ;
#42571=DIRECTION ( 'NONE',  ( 0.7071067811865487940, -0.7071067811865463515, 0.000000000000000000 ) ) ;
#42572=CARTESIAN_POINT ( 'NONE',  ( 6.183988606268994381, 28.73617430169791476, 5.000000000000000000 ) ) ;
#42573=VECTOR ( 'NONE', #77897, 1000.000000000000000 ) ;
#42575=ORIENTED_EDGE ( 'NONE', *, *, #79801, .T. ) ;
#42576=EDGE_CURVE ( 'NONE', #126076, #74252, #6286, .T. ) ;
#42577=LINE ( 'NONE', #131703, #38054 ) ;
#42579=ORIENTED_EDGE ( 'NONE', *, *, #32423, .F. ) ;
#42580=DIRECTION ( 'NONE',  ( -0.000000000000000000, -0.3543493200069152693, 0.9351131265310292928 ) ) ;
#42581=ORIENTED_EDGE ( 'NONE', *, *, #105978, .F. ) ;
#42582=ADVANCED_FACE ( 'NONE', ( #50564 ), #114388, .F. ) ;
#42583=ORIENTED_EDGE ( 'NONE', *, *, #64508, .T. ) ;
#42584=EDGE_LOOP ( 'NONE', ( #18599, #66882, #126293, #109037 ) ) ;
#42585=VECTOR ( 'NONE', #128276, 999.9999999999998863 ) ;
#42587=ORIENTED_EDGE ( 'NONE', *, *, #90195, .T. ) ;
#42588=VERTEX_POINT ( 'NONE', #130998 ) ;
#42590=VECTOR ( 'NONE', #69504, 1000.000000000000000 ) ;
#42591=LINE ( 'NONE', #142596, #5642 ) ;
#42593=LINE ( 'NONE', #142598, #35576 ) ;
#42594=ADVANCED_FACE ( 'NONE', ( #120807 ), #21514, .T. ) ;
#42595=CARTESIAN_POINT ( 'NONE',  ( -42.48921356237308800, -27.52281430457085065, 5.000000000000000000 ) ) ;
#42596=EDGE_LOOP ( 'NONE', ( #63261, #35993, #117319, #137350 ) ) ;
#42597=DIRECTION ( 'NONE',  ( -1.000000000000000000, 0.000000000000000000, 0.000000000000000000 ) ) ;
#42598=EDGE_CURVE ( 'NONE', #31526, #10888, #20779, .T. ) ;
#42599=CARTESIAN_POINT ( 'NONE',  ( 0.000000000000000000, 0.000000000000000000, 5.000000000000000000 ) ) ;
#42600=CARTESIAN_POINT ( 'NONE',  ( -75.18398860626899705, 28.73617430169839793, 5.000000000000000000 ) ) ;
#42604=ORIENTED_EDGE ( 'NONE', *, *, #88027, .T. ) ;
#42606=ORIENTED_EDGE ( 'NONE', *, *, #32757, .F. ) ;
#42608=ORIENTED_EDGE ( 'NONE', *, *, #21551, .T. ) ;
#42609=DIRECTION ( 'NONE',  ( -0.7071067811865487940, 0.7071067811865463515, -0.000000000000000000 ) ) ;
#42610=CARTESIAN_POINT ( 'NONE',  ( 11.99999999999992006, 5.587461875839188075, 4.000000000000000000 ) ) ;
#42611=ORIENTED_EDGE ( 'NONE', *, *, #61249, .F. ) ;
#42612=DIRECTION ( 'NONE',  ( -0.7071067811865487940, 0.7071067811865463515, -0.000000000000000000 ) ) ;
#42613=ORIENTED_EDGE ( 'NONE', *, *, #44347, .F. ) ;
#42614=VECTOR ( 'NONE', #120621, 999.9999999999998863 ) ;
#42615=( BOUNDED_CURVE ( )  B_SPLINE_CURVE ( 3, ( #68657, #91127, #48307, #136025 ),
 .UNSPECIFIED., .F., .T. ) 
 B_SPLINE_CURVE_WITH_KNOTS ( ( 4, 4 ),
 ( 1.208578181583235267, 1.359146454359474232 ),
 .UNSPECIFIED. ) 
 CURVE ( )  GEOMETRIC_REPRESENTATION_ITEM ( )  RATIONAL_B_SPLINE_CURVE ( ( 1.000000000000000000, 0.9981116584018943083, 0.9981116584018943083, 1.000000000000000000 ) ) 
 REPRESENTATION_ITEM ( '' )  );
#42616=ADVANCED_FACE ( 'NONE', ( #9146 ), #118672, .F. ) ;
#42617=EDGE_CURVE ( 'NONE', #55582, #39393, #18617, .T. ) ;
#42618=VECTOR ( 'NONE', #124473, 1000.000000000000227 ) ;
#42620=LINE ( 'NONE', #31712, #62478 ) ;
#42621=DIRECTION ( 'NONE',  ( 0.7071067811865486830, -0.7071067811865464625, -0.000000000000000000 ) ) ;
#42623=ORIENTED_EDGE ( 'NONE', *, *, #71017, .T. ) ;
#42625=VERTEX_POINT ( 'NONE', #130290 ) ;
#42628=CARTESIAN_POINT ( 'NONE',  ( -5.999999999999951150, -3.033600742197705369, 5.000000000000000000 ) ) ;
#42629=ADVANCED_FACE ( 'NONE', ( #32394 ), #140422, .F. ) ;
#42630=VECTOR ( 'NONE', #3833, 1000.000000000000227 ) ;
#42632=CARTESIAN_POINT ( 'NONE',  ( 34.92499999999998295, -13.19990548397269237, 4.759050581649323597 ) ) ;
#42633=DIRECTION ( 'NONE',  ( 0.6830127018922181881, 0.6830127018922202975, -0.2588190451025214056 ) ) ;
#42634=AXIS2_PLACEMENT_3D ( 'NONE', #142112, #42798, #31899 ) ;
#42636=DIRECTION ( 'NONE',  ( 0.7071067811865487940, 0.7071067811865463515, -0.000000000000000000 ) ) ;
#42637=DIRECTION ( 'NONE',  ( -0.7071067811865486830, -0.7071067811865464625, 0.000000000000000000 ) ) ;
#42638=VERTEX_POINT ( 'NONE', #129533 ) ;
#42640=ORIENTED_EDGE ( 'NONE', *, *, #13497, .T. ) ;
#42641=CARTESIAN_POINT ( 'NONE',  ( 69.18398860626899705, 28.73617430169835529, 5.000000000000000000 ) ) ;
#42642=ORIENTED_EDGE ( 'NONE', *, *, #61724, .T. ) ;
#42643=VECTOR ( 'NONE', #105181, 1000.000000000000000 ) ;
#42644=CARTESIAN_POINT ( 'NONE',  ( 33.98911971346028338, -22.02621442084248216, 4.990779571109221102 ) ) ;
#42646=ORIENTED_EDGE ( 'NONE', *, *, #142202, .T. ) ;
#42647=DIRECTION ( 'NONE',  ( -0.6830127018922180770, -0.6830127018922204085, -0.2588190451025213501 ) ) ;
#42648=ORIENTED_EDGE ( 'NONE', *, *, #117390, .T. ) ;
#42649=ORIENTED_EDGE ( 'NONE', *, *, #50542, .F. ) ;
#42650=DIRECTION ( 'NONE',  ( -0.000000000000000000, 0.000000000000000000, 1.000000000000000000 ) ) ;
#42651=ORIENTED_EDGE ( 'NONE', *, *, #63811, .F. ) ;
#42652=VECTOR ( 'NONE', #123527, 1000.000000000000000 ) ;
#42655=CARTESIAN_POINT ( 'NONE',  ( 7.499999999999952927, -4.533600742197692490, 5.000000000000000000 ) ) ;
#42656=VECTOR ( 'NONE', #2428, 1000.000000000000000 ) ;
#42660=EDGE_CURVE ( 'NONE', #41817, #99801, #62897, .T. ) ;
#42665=PLANE ( 'NONE',  #142796 ) ;
#42666=ORIENTED_EDGE ( 'NONE', *, *, #133303, .F. ) ;
#42667=ORIENTED_EDGE ( 'NONE', *, *, #67109, .F. ) ;
#42668=DIRECTION ( 'NONE',  ( -0.000000000000000000, 0.000000000000000000, 1.000000000000000000 ) ) ;
#42669=EDGE_CURVE ( 'NONE', #45818, #74780, #107775, .T. ) ;
#42670=VERTEX_POINT ( 'NONE', #87484 ) ;
#42671=CARTESIAN_POINT ( 'NONE',  ( -26.99999999999980815, 4.384688058510544550, -7.090945410444748020 ) ) ;
#42672=LINE ( 'NONE', #142674, #16079 ) ;
#42673=VECTOR ( 'NONE', #16536, 1000.000000000000000 ) ;
#42675=EDGE_LOOP ( 'NONE', ( #10338, #122171, #53794, #135528 ) ) ;
#42676=DIRECTION ( 'NONE',  ( -0.000000000000000000, 0.3543493200069153248, 0.9351131265310292928 ) ) ;
#42677=DIRECTION ( 'NONE',  ( 0.3543493200069162685, -0.000000000000000000, -0.9351131265310288487 ) ) ;
#42678=ADVANCED_FACE ( 'NONE', ( #120061 ), #31675, .F. ) ;
#42679=DIRECTION ( 'NONE',  ( -0.3543493200069162685, -0.000000000000000000, -0.9351131265310288487 ) ) ;
#42680=EDGE_CURVE ( 'NONE', #72157, #102238, #143279, .T. ) ;
#42681=EDGE_CURVE ( 'NONE', #92779, #136084, #142585, .T. ) ;
#42682=DIRECTION ( 'NONE',  ( 1.000000000000000000, 0.000000000000000000, 0.000000000000000000 ) ) ;
#42683=DIRECTION ( 'NONE',  ( 0.7071067811865486830, -0.7071067811865464625, -0.000000000000000000 ) ) ;
#42686=CARTESIAN_POINT ( 'NONE',  ( -3.792893218813425005, 15.75929247661555799, 5.000000000000000000 ) ) ;
#42687=DIRECTION ( 'NONE',  ( 0.6830127018922180770, -0.6830127018922204085, -0.2588190451025213501 ) ) ;
#42688=FACE_OUTER_BOUND ( 'NONE', #3507, .T. ) ;
#42689=EDGE_CURVE ( 'NONE', #129495, #134514, #86055, .T. ) ;
#42690=ORIENTED_EDGE ( 'NONE', *, *, #61545, .T. ) ;
#42691=ADVANCED_FACE ( 'NONE', ( #141885 ), #97625, .F. ) ;
#42692=ORIENTED_EDGE ( 'NONE', *, *, #64784, .F. ) ;
#42695=VERTEX_POINT ( 'NONE', #64300 ) ;
#42696=EDGE_CURVE ( 'NONE', #62376, #97591, #42577, .T. ) ;
#42698=CARTESIAN_POINT ( 'NONE',  ( -18.29974487139159223, -27.71228299555219010, 4.000000000000000000 ) ) ;
#42699=ORIENTED_EDGE ( 'NONE', *, *, #6826, .F. ) ;
#42701=CARTESIAN_POINT ( 'NONE',  ( -19.49999999999986500, 11.52377502935401310, -1.522421517564041427 ) ) ;
#42702=VECTOR ( 'NONE', #81445, 1000.000000000000000 ) ;
#42703=EDGE_CURVE ( 'NONE', #99005, #108854, #9903, .T. ) ;
#42705=EDGE_LOOP ( 'NONE', ( #134188, #19389, #136492, #103252 ) ) ;
#42706=CARTESIAN_POINT ( 'NONE',  ( -66.48921356237309510, -27.52281430457101763, 5.000000000000000000 ) ) ;
#42709=ORIENTED_EDGE ( 'NONE', *, *, #120732, .F. ) ;
#42710=ORIENTED_EDGE ( 'NONE', *, *, #66289, .F. ) ;
#42711=VERTEX_POINT ( 'NONE', #73738 ) ;
#42712=CARTESIAN_POINT ( 'NONE',  ( -34.92500000000001137, 22.22500000000000142, 4.000000000000000000 ) ) ;
#42713=FACE_OUTER_BOUND ( 'NONE', #67918, .T. ) ;
#42715=DIRECTION ( 'NONE',  ( -0.7071067811865486830, -0.7071067811865464625, 0.000000000000000000 ) ) ;
#42716=VECTOR ( 'NONE', #24025, 999.9999999999998863 ) ;
#42717=ADVANCED_FACE ( 'NONE', ( #108467 ), #53416, .F. ) ;
#42719=DIRECTION ( 'NONE',  ( -0.3543493200069162685, -0.000000000000000000, -0.9351131265310288487 ) ) ;
#42720=AXIS2_PLACEMENT_3D ( 'NONE', #44281, #23943, #88493 ) ;
#42721=ORIENTED_EDGE ( 'NONE', *, *, #44018, .F. ) ;
#42722=ORIENTED_EDGE ( 'NONE', *, *, #108437, .T. ) ;
#42723=VECTOR ( 'NONE', #128581, 1000.000000000000000 ) ;
#42725=VERTEX_POINT ( 'NONE', #88934 ) ;
#42726=ORIENTED_EDGE ( 'NONE', *, *, #126862, .T. ) ;
#42727=EDGE_CURVE ( 'NONE', #27164, #64534, #58481, .T. ) ;
#42728=EDGE_CURVE ( 'NONE', #55336, #51167, #122224, .T. ) ;
#42729=CARTESIAN_POINT ( 'NONE',  ( 4.499999999999968914, -14.56887692260766265, 4.000000000000000000 ) ) ;
#42730=ORIENTED_EDGE ( 'NONE', *, *, #55192, .T. ) ;
#42731=VECTOR ( 'NONE', #23882, 1000.000000000000000 ) ;
#42732=DIRECTION ( 'NONE',  ( -0.000000000000000000, -0.3543493200069152693, 0.9351131265310292928 ) ) ;
#42735=CARTESIAN_POINT ( 'NONE',  ( -14.99999999999989519, 12.25461709320619086, -10.07315571508700458 ) ) ;
#42736=FACE_OUTER_BOUND ( 'NONE', #130735, .T. ) ;
#42739=ORIENTED_EDGE ( 'NONE', *, *, #63632, .F. ) ;
#42740=ADVANCED_FACE ( 'NONE', ( #44740 ), #78754, .F. ) ;
#42742=ORIENTED_EDGE ( 'NONE', *, *, #76377, .F. ) ;
#42743=FACE_OUTER_BOUND ( 'NONE', #18417, .T. ) ;
#42744=ORIENTED_EDGE ( 'NONE', *, *, #53473, .T. ) ;
#42745=DIRECTION ( 'NONE',  ( -0.7071067811865486830, -0.7071067811865464625, 0.000000000000000000 ) ) ;
#42747=CARTESIAN_POINT ( 'NONE',  ( 66.29974487139159578, -27.71228299555252406, 4.000000000000000000 ) ) ;
#42748=VERTEX_POINT ( 'NONE', #47587 ) ;
#42749=VERTEX_POINT ( 'NONE', #1836 ) ;
#42750=EDGE_CURVE ( 'NONE', #127190, #126386, #142166, .T. ) ;
#42751=ORIENTED_EDGE ( 'NONE', *, *, #41097, .F. ) ;
#42752=VECTOR ( 'NONE', #129759, 999.9999999999998863 ) ;
#42756=CARTESIAN_POINT ( 'NONE',  ( -45.48921356237309510, -27.52281430457087197, 5.000000000000000000 ) ) ;
#42757=DIRECTION ( 'NONE',  ( 1.000000000000000000, 0.000000000000000000, 0.000000000000000000 ) ) ;
#42759=AXIS2_PLACEMENT_3D ( 'NONE', #102090, #2755, #111524 ) ;
#42760=EDGE_CURVE ( 'NONE', #35346, #11548, #22896, .T. ) ;
#42763=CARTESIAN_POINT ( 'NONE',  ( -75.48921356237309510, -27.52281430457107803, 5.000000000000000000 ) ) ;
#42764=CARTESIAN_POINT ( 'NONE',  ( 21.77004279457778324, 21.73644205237997795, 5.000000000000000888 ) ) ;
#42765=FACE_OUTER_BOUND ( 'NONE', #58191, .T. ) ;
#42767=ORIENTED_EDGE ( 'NONE', *, *, #129572, .T. ) ;
#42768=ORIENTED_EDGE ( 'NONE', *, *, #113926, .T. ) ;
#42769=ORIENTED_EDGE ( 'NONE', *, *, #134586, .T. ) ;
#42770=DIRECTION ( 'NONE',  ( -0.6830127018922181881, 0.6830127018922202975, -0.2588190451025214056 ) ) ;
#42771=ORIENTED_EDGE ( 'NONE', *, *, #80027, .T. ) ;
#42772=ORIENTED_EDGE ( 'NONE', *, *, #66589, .F. ) ;
#42773=DIRECTION ( 'NONE',  ( -0.000000000000000000, 0.000000000000000000, 1.000000000000000000 ) ) ;
#42774=DIRECTION ( 'NONE',  ( -0.7071067811865486830, 0.7071067811865464625, 0.000000000000000000 ) ) ;
#42775=EDGE_CURVE ( 'NONE', #99771, #137862, #111352, .T. ) ;
#42776=DIRECTION ( 'NONE',  ( -0.000000000000000000, 0.3543493200069153248, 0.9351131265310292928 ) ) ;
#42777=VERTEX_POINT ( 'NONE', #25055 ) ;
#42778=CARTESIAN_POINT ( 'NONE',  ( -3.299744871391591339, -27.71228299555208352, 4.000000000000000000 ) ) ;
#42779=ORIENTED_EDGE ( 'NONE', *, *, #41692, .F. ) ;
#42780=CARTESIAN_POINT ( 'NONE',  ( 0.000000000000000000, 0.000000000000000000, 5.000000000000000000 ) ) ;
#42781=EDGE_CURVE ( 'NONE', #131451, #91250, #23648, .T. ) ;
#42782=DIRECTION ( 'NONE',  ( 1.000000000000000000, 0.000000000000000000, 0.000000000000000000 ) ) ;
#42784=ORIENTED_EDGE ( 'NONE', *, *, #9258, .F. ) ;
#42786=EDGE_CURVE ( 'NONE', #91471, #27362, #134575, .T. ) ;
#42787=FACE_OUTER_BOUND ( 'NONE', #10123, .T. ) ;
#42789=CARTESIAN_POINT ( 'NONE',  ( -27.79333936457828358, 21.75929247661549581, 4.998822639870701856 ) ) ;
#42790=VERTEX_POINT ( 'NONE', #35976 ) ;
#42791=ORIENTED_EDGE ( 'NONE', *, *, #96887, .F. ) ;
#42793=VERTEX_POINT ( 'NONE', #22196 ) ;
#42794=LINE ( 'NONE', #131208, #134290 ) ;
#42795=CARTESIAN_POINT ( 'NONE',  ( -19.49999999999986500, -9.462702396501025959, -9.474982329943468784 ) ) ;
#42796=PLANE ( 'NONE',  #36124 ) ;
#42797=PLANE ( 'NONE',  #135376 ) ;
#42798=DIRECTION ( 'NONE',  ( -0.6830127018922181881, 0.6830127018922202975, -0.2588190451025214056 ) ) ;
#42799=VECTOR ( 'NONE', #23838, 1000.000000000000227 ) ;
#42800=VERTEX_POINT ( 'NONE', #12044 ) ;
#42801=DIRECTION ( 'NONE',  ( -0.000000000000000000, 0.3543493200069152138, -0.9351131265310292928 ) ) ;
#42803=DIRECTION ( 'NONE',  ( -0.7071067811865487940, 0.7071067811865463515, -0.000000000000000000 ) ) ;
#42804=DIRECTION ( 'NONE',  ( 0.7071067811865487940, -0.7071067811865463515, 0.000000000000000000 ) ) ;
#42805=ORIENTED_EDGE ( 'NONE', *, *, #74954, .T. ) ;
#42807=CARTESIAN_POINT ( 'NONE',  ( -7.499999999999940492, 16.46639925780209524, 5.000000000000000000 ) ) ;
#42808=ORIENTED_EDGE ( 'NONE', *, *, #45502, .F. ) ;
#42809=FACE_OUTER_BOUND ( 'NONE', #56154, .T. ) ;
#42811=VERTEX_POINT ( 'NONE', #13452 ) ;
#42813=LINE ( 'NONE', #128382, #97893 ) ;
#42814=CARTESIAN_POINT ( 'NONE',  ( 30.48921356237309510, -27.52281430457076894, 5.000000000000000000 ) ) ;
#42815=EDGE_LOOP ( 'NONE', ( #97268, #54829, #49569, #22676 ) ) ;
#42816=CARTESIAN_POINT ( 'NONE',  ( 17.20710678118641468, -20.24070752338408141, 5.000000000000000000 ) ) ;
#42817=CARTESIAN_POINT ( 'NONE',  ( 14.24139925780194105, 21.72500000000000142, 5.000000000000000000 ) ) ;
#42819=CARTESIAN_POINT ( 'NONE',  ( 8.999999999999937828, -7.068876922607741697, 4.000000000000000000 ) ) ;
#42820=DIRECTION ( 'NONE',  ( -0.7071067811865486830, 0.7071067811865464625, 0.000000000000000000 ) ) ;
#42822=CARTESIAN_POINT ( 'NONE',  ( -63.29974487139158867, -27.71228299555250274, 4.000000000000000000 ) ) ;
#42823=LINE ( 'NONE', #65297, #137501 ) ;
#42824=FACE_OUTER_BOUND ( 'NONE', #77413, .T. ) ;
#42825=CARTESIAN_POINT ( 'NONE',  ( -26.24139925780185578, 21.72500000000000142, 5.000000000000000000 ) ) ;
#42826=CARTESIAN_POINT ( 'NONE',  ( 2.241399257802041856, 21.72499999999999432, 5.000000000000000000 ) ) ;
#42827=CARTESIAN_POINT ( 'NONE',  ( 25.99806943317883068, -22.22500000000000142, 4.500000000000000888 ) ) ;
#42828=FACE_OUTER_BOUND ( 'NONE', #115829, .T. ) ;
#42829=CARTESIAN_POINT ( 'NONE',  ( 28.82816939922333077, 9.759292476615618384, 4.000000000000000000 ) ) ;
#42830=ORIENTED_EDGE ( 'NONE', *, *, #93905, .F. ) ;
#42831=( BOUNDED_CURVE ( )  B_SPLINE_CURVE ( 3, ( #100727, #34762, #54396, #67405 ),
 .UNSPECIFIED., .F., .F. ) 
 B_SPLINE_CURVE_WITH_KNOTS ( ( 4, 4 ),
 ( 5.005968288816724510, 5.074607125596353185 ),
 .UNSPECIFIED. ) 
 CURVE ( )  GEOMETRIC_REPRESENTATION_ITEM ( )  RATIONAL_B_SPLINE_CURVE ( ( 1.000000000000000000, 0.9996074310407762065, 0.9996074310407762065, 1.000000000000000000 ) ) 
 REPRESENTATION_ITEM ( '' )  );
#42832=EDGE_LOOP ( 'NONE', ( #72617, #127678, #124368, #25434 ) ) ;
#42833=ORIENTED_EDGE ( 'NONE', *, *, #70717, .T. ) ;
#42835=ORIENTED_EDGE ( 'NONE', *, *, #33720, .T. ) ;
#42836=VECTOR ( 'NONE', #55463, 999.9999999999998863 ) ;
#42837=EDGE_LOOP ( 'NONE', ( #76298, #33487, #69895, #67744 ) ) ;
#42838=ORIENTED_EDGE ( 'NONE', *, *, #41635, .T. ) ;
#42839=CARTESIAN_POINT ( 'NONE',  ( -28.49999999999980105, 18.43112307739199451, 4.000000000000000000 ) ) ;
#42840=EDGE_CURVE ( 'NONE', #46695, #97392, #35275, .T. ) ;
#42842=ORIENTED_EDGE ( 'NONE', *, *, #59264, .T. ) ;
#42843=( BOUNDED_CURVE ( )  B_SPLINE_CURVE ( 3, ( #100526, #97650, #44759, #143299 ),
 .UNSPECIFIED., .F., .T. ) 
 B_SPLINE_CURVE_WITH_KNOTS ( ( 4, 4 ),
 ( 0.6783063634690170707, 0.7469765549618208045 ),
 .UNSPECIFIED. ) 
 CURVE ( )  GEOMETRIC_REPRESENTATION_ITEM ( )  RATIONAL_B_SPLINE_CURVE ( ( 1.000000000000000000, 0.9996070723374664846, 0.9996070723374664846, 1.000000000000000000 ) ) 
 REPRESENTATION_ITEM ( '' )  );
#42844=CARTESIAN_POINT ( 'NONE',  ( 11.99451991528749417, 28.92564299267946382, 4.000000000000000000 ) ) ;
#42846=PLANE ( 'NONE',  #104241 ) ;
#42847=DIRECTION ( 'NONE',  ( 1.000000000000000000, 0.000000000000000000, 0.000000000000000000 ) ) ;
#42848=ORIENTED_EDGE ( 'NONE', *, *, #105818, .F. ) ;
#42849=EDGE_CURVE ( 'NONE', #38643, #129515, #124387, .T. ) ;
#42850=PLANE ( 'NONE',  #132153 ) ;
#42851=DIRECTION ( 'NONE',  ( 0.7071067811865487940, 0.7071067811865463515, 0.000000000000000000 ) ) ;
#42852=CARTESIAN_POINT ( 'NONE',  ( 1.499999999999992673, 18.43112307739199451, 4.000000000000000000 ) ) ;
#42853=LINE ( 'NONE', #97930, #56742 ) ;
#42857=AXIS2_PLACEMENT_3D ( 'NONE', #23565, #67834, #133077 ) ;
#42858=DIRECTION ( 'NONE',  ( 0.7071067811865487940, 0.7071067811865463515, 0.000000000000000000 ) ) ;
#42859=ADVANCED_FACE ( 'NONE', ( #15575 ), #50408, .F. ) ;
#42860=EDGE_CURVE ( 'NONE', #119020, #64492, #38812, .T. ) ;
#42861=ORIENTED_EDGE ( 'NONE', *, *, #61384, .T. ) ;
#42863=VECTOR ( 'NONE', #22916, 1000.000000000000227 ) ;
#42865=ADVANCED_FACE ( 'NONE', ( #136680 ), #104773, .F. ) ;
#42867=AXIS2_PLACEMENT_3D ( 'NONE', #63244, #107413, #8074 ) ;
#42869=EDGE_CURVE ( 'NONE', #123300, #141915, #103322, .T. ) ;
#42870=CARTESIAN_POINT ( 'NONE',  ( 39.48921356237310221, -27.52281430457082934, 5.000000000000000000 ) ) ;
#42871=EDGE_CURVE ( 'NONE', #79017, #330, #59173, .T. ) ;
#42872=DIRECTION ( 'NONE',  ( 0.7071067811865487940, 0.7071067811865463515, -0.000000000000000000 ) ) ;
#42873=CARTESIAN_POINT ( 'NONE',  ( 28.17183060077628554, 18.75929247661553845, 4.000000000000000000 ) ) ;
#42874=CARTESIAN_POINT ( 'NONE',  ( 0.8500512854102346694, -8.240707523384200428, 17.25253755692239110 ) ) ;
#42876=EDGE_CURVE ( 'NONE', #139000, #35892, #105464, .T. ) ;
#42878=ORIENTED_EDGE ( 'NONE', *, *, #83088, .F. ) ;
#42880=CARTESIAN_POINT ( 'NONE',  ( 2.510786437626908008, -27.52281430457053446, 5.000000000000000000 ) ) ;
#42881=CARTESIAN_POINT ( 'NONE',  ( 31.49999999999979039, 4.466399257802221356, 5.000000000000000000 ) ) ;
#42883=ADVANCED_FACE ( 'NONE', ( #127984 ), #94595, .F. ) ;
#42884=FACE_OUTER_BOUND ( 'NONE', #104239, .T. ) ;
#42885=ORIENTED_EDGE ( 'NONE', *, *, #101805, .T. ) ;
#42887=ORIENTED_EDGE ( 'NONE', *, *, #125704, .F. ) ;
#42888=CARTESIAN_POINT ( 'NONE',  ( 39.18398860626899705, 28.73617430169814568, 5.000000000000000000 ) ) ;
#42889=DIRECTION ( 'NONE',  ( -0.3543493200069162685, -0.000000000000000000, -0.9351131265310288487 ) ) ;
#42890=LINE ( 'NONE', #100103, #20031 ) ;
#42892=EDGE_CURVE ( 'NONE', #74099, #94079, #5433, .T. ) ;
#42894=EDGE_LOOP ( 'NONE', ( #60455, #121686, #57600, #38309 ) ) ;
#42895=FACE_OUTER_BOUND ( 'NONE', #34902, .T. ) ;
#42896=ORIENTED_EDGE ( 'NONE', *, *, #53467, .F. ) ;
#42897=VERTEX_POINT ( 'NONE', #27929 ) ;
#42898=ORIENTED_EDGE ( 'NONE', *, *, #132716, .F. ) ;
#42899=CARTESIAN_POINT ( 'NONE',  ( -34.45011844616454511, 1.516280811637461534, 5.000000000000000888 ) ) ;
#42900=DIRECTION ( 'NONE',  ( 0.7071067811865487940, 0.7071067811865463515, 0.000000000000000000 ) ) ;
#42902=ORIENTED_EDGE ( 'NONE', *, *, #40249, .T. ) ;
#42903=LINE ( 'NONE', #76969, #85309 ) ;
#42904=EDGE_CURVE ( 'NONE', #119580, #15522, #14899, .T. ) ;
#42905=CARTESIAN_POINT ( 'NONE',  ( -35.99451991528749772, 28.92564299267963079, 4.000000000000000000 ) ) ;
#42906=ADVANCED_FACE ( 'NONE', ( #17058 ), #125831, .F. ) ;
#42907=FACE_OUTER_BOUND ( 'NONE', #125122, .T. ) ;
#42908=FACE_BOUND ( 'NONE', #6468, .T. ) ;
#42909=ORIENTED_EDGE ( 'NONE', *, *, #110418, .F. ) ;
#42910=DIRECTION ( 'NONE',  ( -0.7071067811865486830, -0.7071067811865464625, -0.000000000000000000 ) ) ;
#42911=DIRECTION ( 'NONE',  ( -0.6830127018922180770, -0.6830127018922204085, -0.2588190451025213501 ) ) ;
#42912=LINE ( 'NONE', #63938, #129627 ) ;
#42913=ORIENTED_EDGE ( 'NONE', *, *, #47003, .F. ) ;
#42915=ORIENTED_EDGE ( 'NONE', *, *, #82971, .T. ) ;
#42917=EDGE_CURVE ( 'NONE', #122079, #12703, #39543, .T. ) ;
#42918=EDGE_LOOP ( 'NONE', ( #73741, #130986, #85786, #98094 ) ) ;
#42920=ORIENTED_EDGE ( 'NONE', *, *, #24005, .F. ) ;
#42921=LINE ( 'NONE', #21854, #132042 ) ;
#42922=ORIENTED_EDGE ( 'NONE', *, *, #101338, .T. ) ;
#42923=CARTESIAN_POINT ( 'NONE',  ( 5.816011393731002066, 28.73617430169783304, 5.000000000000000000 ) ) ;
#42924=EDGE_CURVE ( 'NONE', #126581, #134968, #27201, .T. ) ;
#42925=DIRECTION ( 'NONE',  ( -0.000000000000000000, -0.3543493200069152693, 0.9351131265310292928 ) ) ;
#42926=ORIENTED_EDGE ( 'NONE', *, *, #80434, .F. ) ;
#42929=PLANE ( 'NONE',  #108053 ) ;
#42930=VECTOR ( 'NONE', #19606, 1000.000000000000227 ) ;
#42931=PLANE ( 'NONE',  #87600 ) ;
#42932=CARTESIAN_POINT ( 'NONE',  ( -33.18398860626899705, 28.73617430169810305, 5.000000000000000000 ) ) ;
#42933=CARTESIAN_POINT ( 'NONE',  ( -12.79289321881336861, 6.759292476615645917, 5.000000000000000000 ) ) ;
#42934=DIRECTION ( 'NONE',  ( 0.6830127018922181881, 0.6830127018922202975, -0.2588190451025214056 ) ) ;
#42935=ORIENTED_EDGE ( 'NONE', *, *, #87182, .F. ) ;
#42937=EDGE_LOOP ( 'NONE', ( #110604, #85702, #31339, #125356, #56123 ) ) ;
#42938=LINE ( 'NONE', #50950, #142263 ) ;
#42939=CARTESIAN_POINT ( 'NONE',  ( -30.48921356237309510, -27.52281430457076894, 5.000000000000000000 ) ) ;
#42940=ORIENTED_EDGE ( 'NONE', *, *, #81548, .T. ) ;
#42941=ORIENTED_EDGE ( 'NONE', *, *, #46428, .T. ) ;
#42943=LINE ( 'NONE', #87143, #20162 ) ;
#42944=ADVANCED_FACE ( 'NONE', ( #72198 ), #137415, .F. ) ;
#42945=EDGE_CURVE ( 'NONE', #5793, #128151, #73500, .T. ) ;
#42946=DIRECTION ( 'NONE',  ( 0.7071067811865486830, -0.7071067811865464625, -0.000000000000000000 ) ) ;
#42948=DIRECTION ( 'NONE',  ( 0.7071067811865487940, -0.7071067811865463515, 0.000000000000000000 ) ) ;
#42950=CARTESIAN_POINT ( 'NONE',  ( -25.49999999999982236, -7.420205493532922247, -2.617629953481312111 ) ) ;
#42952=VECTOR ( 'NONE', #113799, 1000.000000000000000 ) ;
#42953=CARTESIAN_POINT ( 'NONE',  ( -57.48921356237308800, -27.52281430457095368, 5.000000000000000000 ) ) ;
#42954=ORIENTED_EDGE ( 'NONE', *, *, #6618, .F. ) ;
#42957=FACE_OUTER_BOUND ( 'NONE', #16244, .T. ) ;
#42958=PLANE ( 'NONE',  #121352 ) ;
#42960=VERTEX_POINT ( 'NONE', #138124 ) ;
#42961=LINE ( 'NONE', #32065, #141091 ) ;
#42962=VERTEX_POINT ( 'NONE', #75726 ) ;
#42963=AXIS2_PLACEMENT_3D ( 'NONE', #55641, #75265, #75954 ) ;
#42965=DIRECTION ( 'NONE',  ( 0.6830127018922181881, 0.6830127018922202975, -0.2588190451025214056 ) ) ;
#42966=ADVANCED_FACE ( 'NONE', ( #139585 ), #142420, .F. ) ;
#42967=CARTESIAN_POINT ( 'NONE',  ( 27.18398860626900060, 28.73617430169806042, 5.000000000000000000 ) ) ;
#42968=VERTEX_POINT ( 'NONE', #109039 ) ;
#42969=EDGE_CURVE ( 'NONE', #37141, #7710, #117754, .T. ) ;
#42970=EDGE_CURVE ( 'NONE', #142404, #57387, #107619, .T. ) ;
#42972=CARTESIAN_POINT ( 'NONE',  ( -25.01987774928532460, -17.24070752338410983, 20.23474786156463523 ) ) ;
#42973=ORIENTED_EDGE ( 'NONE', *, *, #28679, .F. ) ;
#42974=DIRECTION ( 'NONE',  ( -0.7071067811865486830, -0.7071067811865464625, 0.000000000000000000 ) ) ;
#42975=LINE ( 'NONE', #1547, #35360 ) ;
#42976=ORIENTED_EDGE ( 'NONE', *, *, #85912, .F. ) ;
#42977=LINE ( 'NONE', #9585, #46204 ) ;
#42979=ORIENTED_EDGE ( 'NONE', *, *, #66912, .T. ) ;
#42980=ADVANCED_FACE ( 'NONE', ( #42405 ), #18438, .F. ) ;
#42981=ORIENTED_EDGE ( 'NONE', *, *, #55618, .T. ) ;
#42982=CARTESIAN_POINT ( 'NONE',  ( 57.18398860626899705, 28.73617430169827358, 5.000000000000000000 ) ) ;
#42983=CARTESIAN_POINT ( 'NONE',  ( -66.29974487139159578, -27.71228299555252406, 4.000000000000000000 ) ) ;
#42984=VERTEX_POINT ( 'NONE', #128670 ) ;
#42986=CARTESIAN_POINT ( 'NONE',  ( 23.99999999999982947, -11.35517001088070366, -1.126524801160051714 ) ) ;
#42987=FACE_OUTER_BOUND ( 'NONE', #73295, .T. ) ;
#42988=ORIENTED_EDGE ( 'NONE', *, *, #68952, .F. ) ;
#42989=FACE_OUTER_BOUND ( 'NONE', #38980, .T. ) ;
#42990=FACE_OUTER_BOUND ( 'NONE', #49322, .T. ) ;
#42994=CARTESIAN_POINT ( 'NONE',  ( -2.292986735706930457, -21.74070752338405299, 4.999753212805217117 ) ) ;
#42995=EDGE_LOOP ( 'NONE', ( #63033, #24831, #124697, #134698 ) ) ;
#42996=ORIENTED_EDGE ( 'NONE', *, *, #12709, .F. ) ;
#42997=LINE ( 'NONE', #133569, #90559 ) ;
#42999=ORIENTED_EDGE ( 'NONE', *, *, #68990, .T. ) ;
#43000=CARTESIAN_POINT ( 'NONE',  ( 32.99999999999977263, 4.965500833774359357, -4.007596771432733185 ) ) ;
#43001=CARTESIAN_POINT ( 'NONE',  ( 36.18398860626899705, 28.73617430169812437, 5.000000000000000000 ) ) ;
#43002=ORIENTED_EDGE ( 'NONE', *, *, #12896, .T. ) ;
#43004=PLANE ( 'NONE',  #48919 ) ;
#43005=CARTESIAN_POINT ( 'NONE',  ( -12.18398860626900060, 28.73617430169795739, 5.000000000000000000 ) ) ;
#43006=CARTESIAN_POINT ( 'NONE',  ( -2.292893218813436995, -15.74070752338412049, 5.000000000000000000 ) ) ;
#43008=ORIENTED_EDGE ( 'NONE', *, *, #45645, .F. ) ;
#43009=CARTESIAN_POINT ( 'NONE',  ( 0.000000000000000000, 0.000000000000000000, 5.000000000000000000 ) ) ;
#43011=DIRECTION ( 'NONE',  ( 0.7071067811865487940, -0.7071067811865463515, 0.000000000000000000 ) ) ;
#43012=CARTESIAN_POINT ( 'NONE',  ( 32.29289321881323360, -9.740707523384182664, 5.000000000000000000 ) ) ;
#43013=DIRECTION ( 'NONE',  ( -0.000000000000000000, 0.3543493200069153248, 0.9351131265310292928 ) ) ;
#43014=CARTESIAN_POINT ( 'NONE',  ( -63.18398860626900415, 28.73617430169831621, 5.000000000000000000 ) ) ;
#43016=VECTOR ( 'NONE', #49041, 999.9999999999998863 ) ;
#43018=CARTESIAN_POINT ( 'NONE',  ( 16.82816939922341604, -8.240707523384196875, 4.000000000000000000 ) ) ;
#43019=ORIENTED_EDGE ( 'NONE', *, *, #133361, .T. ) ;
#43020=VERTEX_POINT ( 'NONE', #85152 ) ;
#43022=DIRECTION ( 'NONE',  ( 0.7071067811865486830, -0.7071067811865464625, -0.000000000000000000 ) ) ;
#43023=EDGE_CURVE ( 'NONE', #138242, #52184, #96711, .T. ) ;
#43025=AXIS2_PLACEMENT_3D ( 'NONE', #19844, #87260, #120559 ) ;
#43026=DIRECTION ( 'NONE',  ( 0.6830127018922180770, -0.6830127018922204085, -0.2588190451025213501 ) ) ;
#43027=EDGE_CURVE ( 'NONE', #45976, #13019, #43107, .T. ) ;
#43028=DIRECTION ( 'NONE',  ( 0.7071067811865487940, -0.7071067811865463515, 0.000000000000000000 ) ) ;
#43029=VERTEX_POINT ( 'NONE', #30809 ) ;
#43030=EDGE_CURVE ( 'NONE', #90791, #101471, #140956, .T. ) ;
#43031=CARTESIAN_POINT ( 'NONE',  ( 81.18398860626899705, 28.73617430169844056, 5.000000000000000000 ) ) ;
#43032=CARTESIAN_POINT ( 'NONE',  ( 5.999999999999963585, 14.87792677143809783, -11.06722581663438554 ) ) ;
#43034=VERTEX_POINT ( 'NONE', #64134 ) ;
#43035=EDGE_CURVE ( 'NONE', #14168, #4072, #19889, .T. ) ;
#43036=CARTESIAN_POINT ( 'NONE',  ( -32.20003122016817088, 8.259292476615634371, 16.85664084051848732 ) ) ;
#43037=ORIENTED_EDGE ( 'NONE', *, *, #30792, .F. ) ;
#43038=ORIENTED_EDGE ( 'NONE', *, *, #84309, .T. ) ;
#43039=CARTESIAN_POINT ( 'NONE',  ( 22.49999999999984368, -8.568876922607728375, 4.000000000000000000 ) ) ;
#43040=CARTESIAN_POINT ( 'NONE',  ( -3.722814304570581712, -21.72499999999999432, 5.000000000000000000 ) ) ;
#43041=CARTESIAN_POINT ( 'NONE',  ( -14.67183060077637080, -18.74070752338409562, 4.000000000000000000 ) ) ;
#43042=EDGE_CURVE ( 'NONE', #94963, #110453, #52526, .T. ) ;
#43044=ORIENTED_EDGE ( 'NONE', *, *, #85700, .F. ) ;
#43045=EDGE_CURVE ( 'NONE', #6949, #113816, #75034, .T. ) ;
#43046=CARTESIAN_POINT ( 'NONE',  ( -5.427106230460724490, -22.22500000000000142, 16.17785463845230609 ) ) ;
#43048=VERTEX_POINT ( 'NONE', #106903 ) ;
#43050=CARTESIAN_POINT ( 'NONE',  ( -56.99451991528749062, 28.92564299267978001, 4.000000000000000000 ) ) ;
#43051=LINE ( 'NONE', #129309, #73262 ) ;
#43052=CARTESIAN_POINT ( 'NONE',  ( -6.183988606268994381, 28.73617430169791476, 5.000000000000000000 ) ) ;
#43053=LINE ( 'NONE', #9674, #106494 ) ;
#43055=EDGE_CURVE ( 'NONE', #140430, #135550, #140265, .T. ) ;
#43056=AXIS2_PLACEMENT_3D ( 'NONE', #72313, #38217, #136087 ) ;
#43057=VECTOR ( 'NONE', #82119, 1000.000000000000227 ) ;
#43058=VERTEX_POINT ( 'NONE', #74305 ) ;
#43059=VECTOR ( 'NONE', #88740, 1000.000000000000000 ) ;
#43060=CARTESIAN_POINT ( 'NONE',  ( 21.48921356237309155, -27.52281430457070499, 5.000000000000000000 ) ) ;
#43062=VECTOR ( 'NONE', #107368, 999.9999999999998863 ) ;
#43063=PLANE ( 'NONE',  #55737 ) ;
#43065=DIRECTION ( 'NONE',  ( -0.7071067811865486830, 0.7071067811865464625, 0.000000000000000000 ) ) ;
#43066=ORIENTED_EDGE ( 'NONE', *, *, #75314, .F. ) ;
#43067=ORIENTED_EDGE ( 'NONE', *, *, #21136, .T. ) ;
#43068=VECTOR ( 'NONE', #88826, 1000.000000000000000 ) ;
#43069=FACE_OUTER_BOUND ( 'NONE', #14026, .T. ) ;
#43070=CARTESIAN_POINT ( 'NONE',  ( -57.48921356237308800, -27.52281430457095368, 5.000000000000000000 ) ) ;
#43072=VERTEX_POINT ( 'NONE', #118494 ) ;
#43073=DIRECTION ( 'NONE',  ( -0.000000000000000000, -0.3543493200069152693, 0.9351131265310292928 ) ) ;
#43074=ORIENTED_EDGE ( 'NONE', *, *, #90005, .T. ) ;
#43075=CARTESIAN_POINT ( 'NONE',  ( 34.92499999999998295, 7.512461875839399283, 4.000000000000000000 ) ) ;
#43076=LINE ( 'NONE', #86578, #29456 ) ;
#43077=EDGE_CURVE ( 'NONE', #3834, #43787, #141702, .T. ) ;
#43078=CARTESIAN_POINT ( 'NONE',  ( 45.18398860626900415, 28.73617430169818832, 5.000000000000000000 ) ) ;
#43079=FACE_BOUND ( 'NONE', #87202, .T. ) ;
#43081=CARTESIAN_POINT ( 'NONE',  ( -29.99451991528749417, 28.92564299267958816, 4.000000000000000000 ) ) ;
#43082=DIRECTION ( 'NONE',  ( -0.3543493200069163240, 0.000000000000000000, 0.9351131265310288487 ) ) ;
#43085=EDGE_CURVE ( 'NONE', #65778, #131028, #45970, .T. ) ;
#43086=EDGE_LOOP ( 'NONE', ( #586, #58792, #97106, #79785 ) ) ;
#43089=VERTEX_POINT ( 'NONE', #112628 ) ;
#43090=DIRECTION ( 'NONE',  ( -0.000000000000000000, 0.3543493200069153248, 0.9351131265310292928 ) ) ;
#43091=EDGE_CURVE ( 'NONE', #26613, #25521, #122053, .T. ) ;
#43093=CARTESIAN_POINT ( 'NONE',  ( -24.18398860626899705, 28.73617430169804265, 5.000000000000000000 ) ) ;
#43096=DIRECTION ( 'NONE',  ( -0.3543493200069162685, -0.000000000000000000, -0.9351131265310288487 ) ) ;
#43097=FACE_OUTER_BOUND ( 'NONE', #28229, .T. ) ;
#43098=LINE ( 'NONE', #108291, #91729 ) ;
#43099=ADVANCED_FACE ( 'NONE', ( #11129 ), #10439, .T. ) ;
#43100=LINE ( 'NONE', #40945, #89855 ) ;
#43101=DIRECTION ( 'NONE',  ( 0.7071067811865486830, -0.7071067811865464625, -0.000000000000000000 ) ) ;
#43102=CARTESIAN_POINT ( 'NONE',  ( -51.48921356237309510, -27.52281430457091460, 5.000000000000000000 ) ) ;
#43103=CARTESIAN_POINT ( 'NONE',  ( 2.816011393730999401, 28.73617430169785436, 5.000000000000000000 ) ) ;
#43104=ORIENTED_EDGE ( 'NONE', *, *, #51044, .F. ) ;
#43105=CARTESIAN_POINT ( 'NONE',  ( -26.99999999999980815, -0.8619312979532209873, -5.102805207349888406 ) ) ;
#43106=ORIENTED_EDGE ( 'NONE', *, *, #97898, .T. ) ;
#43107=LINE ( 'NONE', #63451, #116677 ) ;
#43108=LINE ( 'NONE', #87314, #83696 ) ;
#43109=ORIENTED_EDGE ( 'NONE', *, *, #25989, .T. ) ;
#43111=ADVANCED_FACE ( 'NONE', ( #33666 ), #88758, .F. ) ;
#43113=EDGE_LOOP ( 'NONE', ( #19390, #54239, #21583, #122933 ) ) ;
#43115=VECTOR ( 'NONE', #73576, 1000.000000000000000 ) ;
#43116=CARTESIAN_POINT ( 'NONE',  ( 80.99451991528748351, 28.92564299267994699, 4.000000000000000000 ) ) ;
#43119=ORIENTED_EDGE ( 'NONE', *, *, #135070, .T. ) ;
#43121=CARTESIAN_POINT ( 'NONE',  ( 0.000000000000000000, 0.000000000000000000, 5.000000000000000000 ) ) ;
#43122=VERTEX_POINT ( 'NONE', #99584 ) ;
#43123=DIRECTION ( 'NONE',  ( 0.7071067811865487940, 0.7071067811865463515, 0.000000000000000000 ) ) ;
#43124=DIRECTION ( 'NONE',  ( 1.000000000000000000, 0.000000000000000000, 0.000000000000000000 ) ) ;
#43125=VERTEX_POINT ( 'NONE', #264 ) ;
#43126=ORIENTED_EDGE ( 'NONE', *, *, #44322, .F. ) ;
#43127=DIRECTION ( 'NONE',  ( 0.7071067811865487940, -0.7071067811865463515, 0.000000000000000000 ) ) ;
#43130=ORIENTED_EDGE ( 'NONE', *, *, #112087, .F. ) ;
#43131=CARTESIAN_POINT ( 'NONE',  ( -3.005480084712505828, 28.92564299267936079, 4.000000000000000000 ) ) ;
#43132=ORIENTED_EDGE ( 'NONE', *, *, #123740, .T. ) ;
#43133=EDGE_CURVE ( 'NONE', #111536, #128174, #69142, .T. ) ;
#43134=ORIENTED_EDGE ( 'NONE', *, *, #120387, .F. ) ;
#43135=ORIENTED_EDGE ( 'NONE', *, *, #118819, .T. ) ;
#43136=VECTOR ( 'NONE', #37718, 1000.000000000000000 ) ;
#43137=CARTESIAN_POINT ( 'NONE',  ( -60.48921356237309510, -27.52281430457097500, 5.000000000000000000 ) ) ;
#43138=LINE ( 'NONE', #76488, #124888 ) ;
#43142=EDGE_CURVE ( 'NONE', #28852, #138101, #90900, .T. ) ;
#43144=VERTEX_POINT ( 'NONE', #79338 ) ;
#43145=EDGE_CURVE ( 'NONE', #45231, #21649, #68449, .T. ) ;
#43146=CARTESIAN_POINT ( 'NONE',  ( -30.70710678118631876, -12.74070752338415247, 5.000000000000000000 ) ) ;
#43147=EDGE_LOOP ( 'NONE', ( #136408, #140959, #1289, #131257 ) ) ;
#43148=LINE ( 'NONE', #65648, #7731 ) ;
#43149=VECTOR ( 'NONE', #22674, 1000.000000000000000 ) ;
#43151=VECTOR ( 'NONE', #5706, 999.9999999999998863 ) ;
#43152=ORIENTED_EDGE ( 'NONE', *, *, #62911, .T. ) ;
#43153=DIRECTION ( 'NONE',  ( -0.7071067811865486830, -0.7071067811865464625, 0.000000000000000000 ) ) ;
#43154=DIRECTION ( 'NONE',  ( 1.000000000000000000, 0.000000000000000000, 0.000000000000000000 ) ) ;
#43155=LINE ( 'NONE', #40998, #30474 ) ;
#43156=ORIENTED_EDGE ( 'NONE', *, *, #72724, .T. ) ;
#43157=VERTEX_POINT ( 'NONE', #22035 ) ;
#43158=CARTESIAN_POINT ( 'NONE',  ( 3.981552653643277928, 18.75929247661552424, 20.33588619593442104 ) ) ;
#43159=DIRECTION ( 'NONE',  ( -0.000000000000000000, 0.000000000000000000, 1.000000000000000000 ) ) ;
#43160=DIRECTION ( 'NONE',  ( -0.000000000000000000, 0.000000000000000000, 1.000000000000000000 ) ) ;
#43163=CARTESIAN_POINT ( 'NONE',  ( 0.000000000000000000, 0.000000000000000000, 5.000000000000000000 ) ) ;
#43165=EDGE_CURVE ( 'NONE', #18783, #100866, #111175, .T. ) ;
#43166=DIRECTION ( 'NONE',  ( 0.7071067811865487940, 0.7071067811865463515, 0.000000000000000000 ) ) ;
#43168=DIRECTION ( 'NONE',  ( -0.7071067811865486830, 0.7071067811865464625, 0.000000000000000000 ) ) ;
#43169=DIRECTION ( 'NONE',  ( 0.7071067811865486830, -0.7071067811865464625, -0.000000000000000000 ) ) ;
#43170=ORIENTED_EDGE ( 'NONE', *, *, #118139, .F. ) ;
#43171=DIRECTION ( 'NONE',  ( -0.7071067811865487940, 0.7071067811865463515, -0.000000000000000000 ) ) ;
#43172=ORIENTED_EDGE ( 'NONE', *, *, #117963, .T. ) ;
#43173=CARTESIAN_POINT ( 'NONE',  ( 14.70025512860841133, -27.71228299555195917, 4.000000000000000000 ) ) ;
#43174=CARTESIAN_POINT ( 'NONE',  ( 32.90156419391743725, 11.25929247661560950, 10.79108189686414399 ) ) ;
#43175=ORIENTED_EDGE ( 'NONE', *, *, #97347, .F. ) ;
#43176=CARTESIAN_POINT ( 'NONE',  ( 31.49999999999978684, -20.53675388469227414, 2.352720554255964380 ) ) ;
#43177=LINE ( 'NONE', #85952, #118313 ) ;
#43178=ORIENTED_EDGE ( 'NONE', *, *, #93110, .F. ) ;
#43180=CARTESIAN_POINT ( 'NONE',  ( -12.48921356237309155, -27.52281430457064104, 5.000000000000000000 ) ) ;
#43181=FACE_OUTER_BOUND ( 'NONE', #35037, .T. ) ;
#43182=ORIENTED_EDGE ( 'NONE', *, *, #38312, .F. ) ;
#43183=ORIENTED_EDGE ( 'NONE', *, *, #55299, .T. ) ;
#43184=LINE ( 'NONE', #109129, #83400 ) ;
#43185=DIRECTION ( 'NONE',  ( 0.7071067811865486830, -0.7071067811865464625, -0.000000000000000000 ) ) ;
#43186=EDGE_CURVE ( 'NONE', #14957, #138468, #138271, .T. ) ;
#43187=CARTESIAN_POINT ( 'NONE',  ( -5.999999999999963585, 7.588810512006205933, -3.013526669885213227 ) ) ;
#43188=CARTESIAN_POINT ( 'NONE',  ( -27.29974487139158512, -27.71228299555225405, 4.000000000000000000 ) ) ;
#43190=DIRECTION ( 'NONE',  ( -0.7071067811865486830, 0.7071067811865464625, 0.000000000000000000 ) ) ;
#43191=EDGE_CURVE ( 'NONE', #105889, #66880, #8645, .T. ) ;
#43193=CARTESIAN_POINT ( 'NONE',  ( -12.00548008471251293, 28.92564299267929684, 4.000000000000000000 ) ) ;
#43194=ORIENTED_EDGE ( 'NONE', *, *, #102887, .F. ) ;
#43196=PLANE ( 'NONE',  #49298 ) ;
#43197=EDGE_CURVE ( 'NONE', #10130, #30937, #2403, .T. ) ;
#43198=FACE_OUTER_BOUND ( 'NONE', #93454, .T. ) ;
#43199=DIRECTION ( 'NONE',  ( -0.000000000000000000, 0.3543493200069153248, 0.9351131265310292928 ) ) ;
#43200=AXIS2_PLACEMENT_3D ( 'NONE', #29441, #64234, #108395 ) ;
#43201=VERTEX_POINT ( 'NONE', #54696 ) ;
#43202=ADVANCED_FACE ( 'NONE', ( #100334 ), #78580, .T. ) ;
#43205=ORIENTED_EDGE ( 'NONE', *, *, #139127, .T. ) ;
#43207=CARTESIAN_POINT ( 'NONE',  ( -0.1839886062690032631, 28.73617430169787568, 5.000000000000000000 ) ) ;
#43209=ORIENTED_EDGE ( 'NONE', *, *, #67622, .T. ) ;
#43210=DIRECTION ( 'NONE',  ( 0.3543493200069162685, -0.000000000000000000, -0.9351131265310288487 ) ) ;
#43211=FACE_OUTER_BOUND ( 'NONE', #136805, .T. ) ;
#43212=CARTESIAN_POINT ( 'NONE',  ( 45.48921356237309510, -27.52281430457087197, 5.000000000000000000 ) ) ;
#43213=EDGE_CURVE ( 'NONE', #48454, #3971, #132987, .T. ) ;
#43214=DIRECTION ( 'NONE',  ( 0.7071067811865487940, 0.7071067811865463515, -0.000000000000000000 ) ) ;
#43215=EDGE_CURVE ( 'NONE', #94724, #119206, #56867, .T. ) ;
#43216=DIRECTION ( 'NONE',  ( -0.7071067811865486830, -0.7071067811865464625, -0.000000000000000000 ) ) ;
#43217=ORIENTED_EDGE ( 'NONE', *, *, #70993, .T. ) ;
#43218=CARTESIAN_POINT ( 'NONE',  ( 28.49999999999980105, -13.91253812416061564, 4.000000000000000000 ) ) ;
#43220=DIRECTION ( 'NONE',  ( -0.7071067811865486830, 0.7071067811865464625, 0.000000000000000000 ) ) ;
#43222=VERTEX_POINT ( 'NONE', #138679 ) ;
#43223=EDGE_CURVE ( 'NONE', #84277, #131836, #114132, .T. ) ;
#43224=ORIENTED_EDGE ( 'NONE', *, *, #34780, .T. ) ;
#43227=VECTOR ( 'NONE', #119499, 1000.000000000000000 ) ;
#43229=DIRECTION ( 'NONE',  ( 0.7071067811865487940, 0.7071067811865463515, 0.000000000000000000 ) ) ;
#43231=CARTESIAN_POINT ( 'NONE',  ( 24.58521188482543707, 5.410383847852841654, 4.279600586820021313 ) ) ;
#43232=CARTESIAN_POINT ( 'NONE',  ( -36.48921356237310221, -27.52281430457080802, 5.000000000000000000 ) ) ;
#43233=VERTEX_POINT ( 'NONE', #49546 ) ;
#43234=VERTEX_POINT ( 'NONE', #83591 ) ;
#43235=EDGE_CURVE ( 'NONE', #115217, #58332, #26340, .T. ) ;
#43236=DIRECTION ( 'NONE',  ( 0.3543493200069163240, -0.000000000000000000, 0.9351131265310288487 ) ) ;
#43237=DIRECTION ( 'NONE',  ( -0.6830127018922180770, -0.6830127018922204085, -0.2588190451025213501 ) ) ;
#43238=ORIENTED_EDGE ( 'NONE', *, *, #37881, .F. ) ;
#43239=AXIS2_PLACEMENT_3D ( 'NONE', #90308, #84465, #50393 ) ;
#43240=LINE ( 'NONE', #22859, #67488 ) ;
#43241=LINE ( 'NONE', #9109, #24700 ) ;
#43242=EDGE_CURVE ( 'NONE', #35082, #116175, #59694, .T. ) ;
#43245=AXIS2_PLACEMENT_3D ( 'NONE', #31462, #87265, #30760 ) ;
#43246=FACE_OUTER_BOUND ( 'NONE', #95266, .T. ) ;
#43247=FACE_OUTER_BOUND ( 'NONE', #35507, .T. ) ;
#43248=ADVANCED_FACE ( 'NONE', ( #104601 ), #93017, .F. ) ;
#43249=DIRECTION ( 'NONE',  ( 0.7071067811865486830, -0.7071067811865464625, -0.000000000000000000 ) ) ;
#43250=CARTESIAN_POINT ( 'NONE',  ( 17.24139925780192328, 21.72500000000000142, 5.000000000000000000 ) ) ;
#43251=EDGE_CURVE ( 'NONE', #134235, #141074, #81459, .T. ) ;
#43252=DIRECTION ( 'NONE',  ( 1.000000000000000000, 0.000000000000000000, 0.000000000000000000 ) ) ;
#43258=ORIENTED_EDGE ( 'NONE', *, *, #110630, .T. ) ;
#43259=VECTOR ( 'NONE', #91528, 1000.000000000000000 ) ;
#43260=ORIENTED_EDGE ( 'NONE', *, *, #123353, .T. ) ;
#43263=ORIENTED_EDGE ( 'NONE', *, *, #98828, .T. ) ;
#43264=AXIS2_PLACEMENT_3D ( 'NONE', #14286, #56417, #58571 ) ;
#43265=LINE ( 'NONE', #108452, #16662 ) ;
#43266=FACE_OUTER_BOUND ( 'NONE', #13052, .T. ) ;
#43267=CARTESIAN_POINT ( 'NONE',  ( -63.29974487139158867, -27.71228299555250274, 4.000000000000000000 ) ) ;
#43268=EDGE_LOOP ( 'NONE', ( #108855, #31287, #92055, #59139 ) ) ;
#43269=CARTESIAN_POINT ( 'NONE',  ( -6.183988606268994381, 28.73617430169791476, 5.000000000000000000 ) ) ;
#43270=DIRECTION ( 'NONE',  ( -0.7071067811865487940, 0.7071067811865463515, -0.000000000000000000 ) ) ;
#43271=LINE ( 'NONE', #86771, #8641 ) ;
#43272=CARTESIAN_POINT ( 'NONE',  ( -20.99999999999984368, 8.816494571476647835, 4.604407763760409722 ) ) ;
#43273=CARTESIAN_POINT ( 'NONE',  ( 9.717577386425601205, -21.73023691814493930, 5.000000000000000888 ) ) ;
#43275=EDGE_LOOP ( 'NONE', ( #120400, #52451, #12111, #108849 ) ) ;
#43276=CARTESIAN_POINT ( 'NONE',  ( -69.48921356237309510, -27.52281430457103895, 5.000000000000000000 ) ) ;
#43277=DIRECTION ( 'NONE',  ( -0.7071067811865486830, -0.7071067811865464625, 0.000000000000000000 ) ) ;
#43278=ORIENTED_EDGE ( 'NONE', *, *, #109152, .T. ) ;
#43280=EDGE_LOOP ( 'NONE', ( #13943, #42608, #120872, #19234 ) ) ;
#43282=VECTOR ( 'NONE', #135308, 1000.000000000000114 ) ;
#43283=ORIENTED_EDGE ( 'NONE', *, *, #2361, .T. ) ;
#43284=DIRECTION ( 'NONE',  ( 0.6830127018922180770, -0.6830127018922204085, -0.2588190451025213501 ) ) ;
#43285=VECTOR ( 'NONE', #56975, 1000.000000000000000 ) ;
#43288=CARTESIAN_POINT ( 'NONE',  ( 0.1839886062690032631, 28.73617430169787568, 5.000000000000000000 ) ) ;
#43289=ORIENTED_EDGE ( 'NONE', *, *, #20642, .T. ) ;
#43293=CARTESIAN_POINT ( 'NONE',  ( 14.91508676806229516, -12.74070752338415247, 18.74364270924357712 ) ) ;
#43294=ORIENTED_EDGE ( 'NONE', *, *, #46501, .F. ) ;
#43295=DIRECTION ( 'NONE',  ( -0.7071067811865487940, 0.7071067811865463515, 0.000000000000000000 ) ) ;
#43296=VERTEX_POINT ( 'NONE', #47427 ) ;
#43297=ORIENTED_EDGE ( 'NONE', *, *, #16848, .T. ) ;
#43298=ORIENTED_EDGE ( 'NONE', *, *, #47632, .T. ) ;
#43300=VECTOR ( 'NONE', #83479, 1000.000000000000000 ) ;
#43301=ORIENTED_EDGE ( 'NONE', *, *, #114205, .F. ) ;
#43302=DIRECTION ( 'NONE',  ( 0.7071067811865487940, -0.7071067811865463515, 0.000000000000000000 ) ) ;
#43303=AXIS2_PLACEMENT_3D ( 'NONE', #22519, #110247, #10927 ) ;
#43308=LINE ( 'NONE', #109970, #125241 ) ;
#43309=ORIENTED_EDGE ( 'NONE', *, *, #55817, .F. ) ;
#43310=VECTOR ( 'NONE', #142245, 1000.000000000000000 ) ;
#43313=FACE_OUTER_BOUND ( 'NONE', #11107, .T. ) ;
#43314=VECTOR ( 'NONE', #101166, 1000.000000000000227 ) ;
#43317=ORIENTED_EDGE ( 'NONE', *, *, #52655, .F. ) ;
#43318=ORIENTED_EDGE ( 'NONE', *, *, #45048, .T. ) ;
#43319=ORIENTED_EDGE ( 'NONE', *, *, #23525, .F. ) ;
#43321=DIRECTION ( 'NONE',  ( -0.7071067811865486830, -0.7071067811865464625, 0.000000000000000000 ) ) ;
#43322=LINE ( 'NONE', #56378, #79814 ) ;
#43323=LINE ( 'NONE', #142631, #48288 ) ;
#43325=DIRECTION ( 'NONE',  ( 0.6830127018922181881, 0.6830127018922202975, -0.2588190451025214056 ) ) ;
#43327=LINE ( 'NONE', #78814, #55959 ) ;
#43328=CYLINDRICAL_SURFACE ( 'NONE', #109060, 0.5000000000000004441 ) ;
#43329=VERTEX_POINT ( 'NONE', #72016 ) ;
#43334=ORIENTED_EDGE ( 'NONE', *, *, #131425, .T. ) ;
#43335=LINE ( 'NONE', #100574, #99200 ) ;
#43336=CARTESIAN_POINT ( 'NONE',  ( -54.18398860626899705, 28.73617430169825226, 5.000000000000000000 ) ) ;
#43337=ORIENTED_EDGE ( 'NONE', *, *, #82678, .T. ) ;
#43338=AXIS2_PLACEMENT_3D ( 'NONE', #68753, #47041, #133987 ) ;
#43339=CARTESIAN_POINT ( 'NONE',  ( 8.999999999999937828, -9.033600742197648970, 5.000000000000000000 ) ) ;
#43340=ORIENTED_EDGE ( 'NONE', *, *, #102721, .F. ) ;
#43341=VERTEX_POINT ( 'NONE', #116196 ) ;
#43342=CARTESIAN_POINT ( 'NONE',  ( 26.99451991528749417, 28.92564299267956685, 4.000000000000000000 ) ) ;
#43343=ORIENTED_EDGE ( 'NONE', *, *, #125327, .F. ) ;
#43344=VECTOR ( 'NONE', #79303, 1000.000000000000000 ) ;
#43345=VECTOR ( 'NONE', #31822, 1000.000000000000000 ) ;
#43349=CARTESIAN_POINT ( 'NONE',  ( 29.99999999999979750, 7.552185695429093570, 5.000000000000000000 ) ) ;
#43350=CARTESIAN_POINT ( 'NONE',  ( 0.000000000000000000, 0.000000000000000000, 5.000000000000000000 ) ) ;
#43351=FACE_OUTER_BOUND ( 'NONE', #126721, .T. ) ;
#43352=LINE ( 'NONE', #11381, #5520 ) ;
#43353=EDGE_CURVE ( 'NONE', #94037, #131599, #38641, .T. ) ;
#43358=CARTESIAN_POINT ( 'NONE',  ( 57.29974487139158157, -27.71228299555246011, 4.000000000000000000 ) ) ;
#43359=FACE_OUTER_BOUND ( 'NONE', #70181, .T. ) ;
#43360=ORIENTED_EDGE ( 'NONE', *, *, #2203, .F. ) ;
#43361=EDGE_CURVE ( 'NONE', #96026, #88536, #3137, .T. ) ;
#43362=ORIENTED_EDGE ( 'NONE', *, *, #34099, .F. ) ;
#43363=EDGE_CURVE ( 'NONE', #46867, #6491, #25604, .T. ) ;
#43364=DIRECTION ( 'NONE',  ( 1.000000000000000000, 0.000000000000000000, 0.000000000000000000 ) ) ;
#43365=ORIENTED_EDGE ( 'NONE', *, *, #38419, .T. ) ;
#43366=CARTESIAN_POINT ( 'NONE',  ( 34.92499999999998295, 9.006123077391862353, 4.000000000000000000 ) ) ;
#43369=ADVANCED_FACE ( 'NONE', ( #27036 ), #71282, .F. ) ;
#43370=DIRECTION ( 'NONE',  ( 0.7071067811865487940, 0.7071067811865463515, -0.000000000000000000 ) ) ;
#43371=FACE_OUTER_BOUND ( 'NONE', #48120, .T. ) ;
#43372=CARTESIAN_POINT ( 'NONE',  ( 22.49999999999984368, -4.796895815300995736, -3.611700055028630896 ) ) ;
#43373=EDGE_CURVE ( 'NONE', #75148, #102362, #50238, .T. ) ;
#43376=PLANE ( 'NONE',  #61366 ) ;
#43377=ORIENTED_EDGE ( 'NONE', *, *, #117886, .F. ) ;
#43378=LINE ( 'NONE', #86883, #74444 ) ;
#43379=VECTOR ( 'NONE', #118510, 1000.000000000000000 ) ;
#43380=PLANE ( 'NONE',  #36017 ) ;
#43381=DIRECTION ( 'NONE',  ( -0.7071067811865486830, -0.7071067811865464625, -0.000000000000000000 ) ) ;
#43382=LINE ( 'NONE', #65883, #95479 ) ;
#43383=EDGE_LOOP ( 'NONE', ( #115965, #96531, #61473, #95142 ) ) ;
#43384=ORIENTED_EDGE ( 'NONE', *, *, #62846, .F. ) ;
#43385=ORIENTED_EDGE ( 'NONE', *, *, #71832, .T. ) ;
#43387=( BOUNDED_CURVE ( )  B_SPLINE_CURVE ( 3, ( #100631, #33269, #1279, #143402 ),
 .UNSPECIFIED., .F., .T. ) 
 B_SPLINE_CURVE_WITH_KNOTS ( ( 4, 4 ),
 ( 4.735358278776982566, 4.752060726170251215 ),
 .UNSPECIFIED. ) 
 CURVE ( )  GEOMETRIC_REPRESENTATION_ITEM ( )  RATIONAL_B_SPLINE_CURVE ( ( 1.000000000000000000, 0.9999767524893692361, 0.9999767524893692361, 1.000000000000000000 ) ) 
 REPRESENTATION_ITEM ( '' )  );
#43388=EDGE_LOOP ( 'NONE', ( #104515, #90814, #27383, #110265 ) ) ;
#43389=EDGE_CURVE ( 'NONE', #33213, #66785, #108136, .T. ) ;
#43391=VECTOR ( 'NONE', #35402, 1000.000000000000000 ) ;
#43392=CARTESIAN_POINT ( 'NONE',  ( 5.292893218813425449, -9.740707523384184441, 5.000000000000000000 ) ) ;
#43393=ORIENTED_EDGE ( 'NONE', *, *, #127916, .F. ) ;
#43394=EDGE_CURVE ( 'NONE', #1311, #32610, #61838, .T. ) ;
#43395=FACE_OUTER_BOUND ( 'NONE', #89650, .T. ) ;
#43396=LINE ( 'NONE', #20178, #55864 ) ;
#43398=VERTEX_POINT ( 'NONE', #7408 ) ;
#43399=DIRECTION ( 'NONE',  ( 0.7071067811865487940, 0.7071067811865463515, -0.000000000000000000 ) ) ;
#43402=ORIENTED_EDGE ( 'NONE', *, *, #80680, .F. ) ;
#43403=EDGE_LOOP ( 'NONE', ( #43788, #116965, #71747, #12449 ) ) ;
#43405=CARTESIAN_POINT ( 'NONE',  ( 51.48921356237309510, -27.52281430457091460, 5.000000000000000000 ) ) ;
#43406=LINE ( 'NONE', #141273, #112642 ) ;
#43408=CARTESIAN_POINT ( 'NONE',  ( 0.000000000000000000, 0.000000000000000000, 5.000000000000000000 ) ) ;
#43410=DIRECTION ( 'NONE',  ( -0.6830127018922181881, 0.6830127018922202975, -0.2588190451025214056 ) ) ;
#43411=EDGE_CURVE ( 'NONE', #3513, #8673, #116902, .T. ) ;
#43413=EDGE_CURVE ( 'NONE', #63081, #55039, #85687, .T. ) ;
#43414=ORIENTED_EDGE ( 'NONE', *, *, #4287, .F. ) ;
#43417=PLANE ( 'NONE',  #61886 ) ;
#43418=ORIENTED_EDGE ( 'NONE', *, *, #112576, .F. ) ;
#43420=EDGE_CURVE ( 'NONE', #89257, #64833, #129929, .T. ) ;
#43421=AXIS2_PLACEMENT_3D ( 'NONE', #43713, #99492, #77782 ) ;
#43422=DIRECTION ( 'NONE',  ( -0.3543493200069162685, -0.000000000000000000, -0.9351131265310288487 ) ) ;
#43423=EDGE_LOOP ( 'NONE', ( #140290, #7013, #10561 ) ) ;
#43427=DIRECTION ( 'NONE',  ( 1.000000000000000000, 0.000000000000000000, 0.000000000000000000 ) ) ;
#43429=DIRECTION ( 'NONE',  ( -0.7071067811865486830, 0.7071067811865464625, -0.000000000000000000 ) ) ;
#43430=VERTEX_POINT ( 'NONE', #9542 ) ;
#43431=LINE ( 'NONE', #84789, #23307 ) ;
#43432=EDGE_LOOP ( 'NONE', ( #107194, #27398, #99360, #44899 ) ) ;
#43434=ORIENTED_EDGE ( 'NONE', *, *, #21501, .T. ) ;
#43437=CARTESIAN_POINT ( 'NONE',  ( -4.499999999999968914, 14.14708470758590764, -0.5283514160166454809 ) ) ;
#43438=EDGE_LOOP ( 'NONE', ( #53200, #125121, #129098, #54475 ) ) ;
#43439=VERTEX_POINT ( 'NONE', #41474 ) ;
#43441=EDGE_LOOP ( 'NONE', ( #27018, #15421, #118352, #50687 ) ) ;
#43443=VECTOR ( 'NONE', #38229, 1000.000000000000000 ) ;
#43444=CARTESIAN_POINT ( 'NONE',  ( 66.48921356237309510, -27.52281430457101763, 5.000000000000000000 ) ) ;
#43445=LINE ( 'NONE', #110104, #27511 ) ;
#43446=DIRECTION ( 'NONE',  ( 0.7071067811865486830, -0.7071067811865464625, -0.000000000000000000 ) ) ;
#43447=DIRECTION ( 'NONE',  ( -0.7071067811865486830, -0.7071067811865464625, 0.000000000000000000 ) ) ;
#43448=CARTESIAN_POINT ( 'NONE',  ( -12.70710678118645909, 8.259292476615636147, 5.000000000000000000 ) ) ;
#43450=EDGE_CURVE ( 'NONE', #86643, #50077, #88323, .T. ) ;
#43451=DIRECTION ( 'NONE',  ( -0.3543493200069163240, -0.000000000000000000, 0.9351131265310288487 ) ) ;
#43452=LINE ( 'NONE', #143461, #141869 ) ;
#43453=CARTESIAN_POINT ( 'NONE',  ( 18.18398860626898994, 28.73617430169800002, 5.000000000000000000 ) ) ;
#43455=CARTESIAN_POINT ( 'NONE',  ( 2.994519915287485734, 28.92564299267940342, 4.000000000000000000 ) ) ;
#43456=ORIENTED_EDGE ( 'NONE', *, *, #74363, .F. ) ;
#43457=ORIENTED_EDGE ( 'NONE', *, *, #41539, .T. ) ;
#43458=ORIENTED_EDGE ( 'NONE', *, *, #61617, .F. ) ;
#43459=CARTESIAN_POINT ( 'NONE',  ( 11.20710678118646797, 15.75929247661555976, 5.000000000000000000 ) ) ;
#43460=VERTEX_POINT ( 'NONE', #119039 ) ;
#43461=ADVANCED_FACE ( 'NONE', ( #53057 ), #84314, .T. ) ;
#43462=EDGE_LOOP ( 'NONE', ( #71775, #3814, #1102, #89208 ) ) ;
#43463=DIRECTION ( 'NONE',  ( -0.7071067811865487940, 0.7071067811865463515, -0.000000000000000000 ) ) ;
#43464=CARTESIAN_POINT ( 'NONE',  ( 10.49999999999993605, 16.46639925780209524, 5.000000000000000000 ) ) ;
#43465=EDGE_CURVE ( 'NONE', #1803, #11699, #29878, .T. ) ;
#43466=CARTESIAN_POINT ( 'NONE',  ( 30.48921356237309510, -27.52281430457076894, 5.000000000000000000 ) ) ;
#43467=VERTEX_POINT ( 'NONE', #98018 ) ;
#43468=AXIS2_PLACEMENT_3D ( 'NONE', #38658, #82888, #131695 ) ;
#43469=CARTESIAN_POINT ( 'NONE',  ( -66.18398860626901126, 28.73617430169833753, 5.000000000000000000 ) ) ;
#43470=ORIENTED_EDGE ( 'NONE', *, *, #27940, .T. ) ;
#43471=PLANE ( 'NONE',  #76962 ) ;
#43472=EDGE_CURVE ( 'NONE', #75329, #61250, #42938, .T. ) ;
#43474=FACE_OUTER_BOUND ( 'NONE', #30737, .T. ) ;
#43477=VERTEX_POINT ( 'NONE', #29179 ) ;
#43481=PLANE ( 'NONE',  #106834 ) ;
#43482=LINE ( 'NONE', #87693, #25701 ) ;
#43483=VERTEX_POINT ( 'NONE', #95861 ) ;
#43485=EDGE_LOOP ( 'NONE', ( #133572, #142327, #115421, #113660 ) ) ;
#43486=FACE_OUTER_BOUND ( 'NONE', #139227, .T. ) ;
#43487=DIRECTION ( 'NONE',  ( 0.7071067811865486830, -0.7071067811865464625, -0.000000000000000000 ) ) ;
#43488=LINE ( 'NONE', #65989, #86710 ) ;
#43489=ORIENTED_EDGE ( 'NONE', *, *, #35989, .F. ) ;
#43490=DIRECTION ( 'NONE',  ( -0.3543493200069162685, -0.000000000000000000, -0.9351131265310288487 ) ) ;
#43491=EDGE_CURVE ( 'NONE', #133481, #111466, #140108, .T. ) ;
#43492=FACE_OUTER_BOUND ( 'NONE', #62771, .T. ) ;
#43494=ORIENTED_EDGE ( 'NONE', *, *, #31901, .F. ) ;
#43495=CARTESIAN_POINT ( 'NONE',  ( 7.499999999999940492, -14.56887692260766443, 4.000000000000000000 ) ) ;
#43496=EDGE_CURVE ( 'NONE', #89022, #37569, #19021, .T. ) ;
#43497=CARTESIAN_POINT ( 'NONE',  ( -33.70710678118631165, 20.25929247661551713, 5.000000000000000000 ) ) ;
#43498=EDGE_LOOP ( 'NONE', ( #31315, #10286, #8855, #99210 ) ) ;
#43499=DIRECTION ( 'NONE',  ( -0.7071067811865487940, 0.7071067811865463515, -0.000000000000000000 ) ) ;
#43500=EDGE_LOOP ( 'NONE', ( #107245, #65034, #31988, #134595 ) ) ;
#43501=EDGE_LOOP ( 'NONE', ( #121487, #106453, #120983, #66241 ) ) ;
#43502=LINE ( 'NONE', #55832, #60993 ) ;
#43504=EDGE_CURVE ( 'NONE', #94991, #118382, #55226, .T. ) ;
#43506=CARTESIAN_POINT ( 'NONE',  ( 12.48921356237309155, -27.52281430457064104, 5.000000000000000000 ) ) ;
#43508=LINE ( 'NONE', #121056, #114608 ) ;
#43510=CARTESIAN_POINT ( 'NONE',  ( -15.48921356237309510, -27.52281430457066236, 5.000000000000000000 ) ) ;
#43512=DIRECTION ( 'NONE',  ( 0.7071067811865486830, -0.7071067811865464625, -0.000000000000000000 ) ) ;
#43513=LINE ( 'NONE', #100048, #116576 ) ;
#43514=EDGE_CURVE ( 'NONE', #29884, #16309, #67555, .T. ) ;
#43515=PLANE ( 'NONE',  #71529 ) ;
#43516=CARTESIAN_POINT ( 'NONE',  ( 0.7928932188134502068, 18.75929247661552779, 5.000000000000000000 ) ) ;
#43518=DIRECTION ( 'NONE',  ( -0.6830127018922181881, 0.6830127018922202975, -0.2588190451025214056 ) ) ;
#43520=CARTESIAN_POINT ( 'NONE',  ( -34.17183060077623225, -14.24070752338413293, 4.000000000000000000 ) ) ;
#43522=ORIENTED_EDGE ( 'NONE', *, *, #12634, .F. ) ;
#43523=ADVANCED_FACE ( 'NONE', ( #100165 ), #45104, .F. ) ;
#43525=VECTOR ( 'NONE', #92194, 1000.000000000000000 ) ;
#43526=ORIENTED_EDGE ( 'NONE', *, *, #39170, .T. ) ;
#43527=ORIENTED_EDGE ( 'NONE', *, *, #36977, .T. ) ;
#43528=EDGE_CURVE ( 'NONE', #10002, #37807, #123359, .T. ) ;
#43529=ORIENTED_EDGE ( 'NONE', *, *, #66169, .F. ) ;
#43530=LINE ( 'NONE', #19631, #24761 ) ;
#43531=DIRECTION ( 'NONE',  ( 1.000000000000000000, 0.000000000000000000, 0.000000000000000000 ) ) ;
#43532=VERTEX_POINT ( 'NONE', #814 ) ;
#43533=VECTOR ( 'NONE', #85175, 1000.000000000000000 ) ;
#43534=CARTESIAN_POINT ( 'NONE',  ( -4.499999999999962697, 8.319652575858382804, -8.582050562765838109 ) ) ;
#43535=EDGE_CURVE ( 'NONE', #92108, #26770, #21160, .T. ) ;
#43536=CARTESIAN_POINT ( 'NONE',  ( -24.18398860626899705, 28.73617430169804265, 5.000000000000000000 ) ) ;
#43537=VECTOR ( 'NONE', #28464, 1000.000000000000000 ) ;
#43538=DIRECTION ( 'NONE',  ( -0.7071067811865486830, -0.7071067811865464625, 0.000000000000000000 ) ) ;
#43539=CARTESIAN_POINT ( 'NONE',  ( -34.64175702458838657, 15.75929247661555088, 19.34181609438707738 ) ) ;
#43540=ORIENTED_EDGE ( 'NONE', *, *, #107764, .F. ) ;
#43541=LINE ( 'NONE', #74771, #18684 ) ;
#43542=DIRECTION ( 'NONE',  ( 1.000000000000000000, 0.000000000000000000, 0.000000000000000000 ) ) ;
#43544=DIRECTION ( 'NONE',  ( 0.6830127018922180770, -0.6830127018922204085, -0.2588190451025213501 ) ) ;
#43545=CARTESIAN_POINT ( 'NONE',  ( 8.999999999999937828, 18.08204922493374767, 0.9627537363044690322 ) ) ;
#43546=DIRECTION ( 'NONE',  ( -0.7071067811865487940, 0.7071067811865463515, -0.000000000000000000 ) ) ;
#43548=LINE ( 'NONE', #55151, #79305 ) ;
#43550=ORIENTED_EDGE ( 'NONE', *, *, #109366, .F. ) ;
#43552=EDGE_LOOP ( 'NONE', ( #98572, #77869, #131187, #13926 ) ) ;
#43553=EDGE_CURVE ( 'NONE', #132816, #2809, #89278, .T. ) ;
#43554=PLANE ( 'NONE',  #18484 ) ;
#43555=LINE ( 'NONE', #20350, #94177 ) ;
#43556=CARTESIAN_POINT ( 'NONE',  ( -27.48921356237309155, -27.52281430457074762, 5.000000000000000000 ) ) ;
#43557=EDGE_CURVE ( 'NONE', #64166, #11127, #133504, .T. ) ;
#43559=LINE ( 'NONE', #32705, #23487 ) ;
#43562=ORIENTED_EDGE ( 'NONE', *, *, #13274, .F. ) ;
#43563=ORIENTED_EDGE ( 'NONE', *, *, #103934, .T. ) ;
#43564=CARTESIAN_POINT ( 'NONE',  ( -11.99999999999991296, 20.70535890316560312, 1.956823837851944470 ) ) ;
#43565=DIRECTION ( 'NONE',  ( -0.000000000000000000, 0.000000000000000000, 1.000000000000000000 ) ) ;
#43567=VERTEX_POINT ( 'NONE', #122603 ) ;
#43568=ORIENTED_EDGE ( 'NONE', *, *, #44045, .T. ) ;
#43570=ORIENTED_EDGE ( 'NONE', *, *, #10182, .T. ) ;
#43571=FACE_OUTER_BOUND ( 'NONE', #13454, .T. ) ;
#43572=ADVANCED_FACE ( 'NONE', ( #75 ), #44378, .F. ) ;
#43573=DIRECTION ( 'NONE',  ( -0.3543493200069163240, -0.000000000000000000, -0.9351131265310288487 ) ) ;
#43575=CARTESIAN_POINT ( 'NONE',  ( -14.99999999999988098, -22.06887692260758982, 4.000000000000000000 ) ) ;
#43577=ORIENTED_EDGE ( 'NONE', *, *, #92487, .T. ) ;
#43578=CARTESIAN_POINT ( 'NONE',  ( 25.49999999999982592, 12.43112307739206024, 4.000000000000000000 ) ) ;
#43579=VERTEX_POINT ( 'NONE', #13116 ) ;
#43580=VERTEX_POINT ( 'NONE', #54530 ) ;
#43581=VECTOR ( 'NONE', #58668, 1000.000000000000000 ) ;
#43583=EDGE_CURVE ( 'NONE', #104658, #20345, #2223, .T. ) ;
#43584=VECTOR ( 'NONE', #122118, 999.9999999999998863 ) ;
#43585=EDGE_CURVE ( 'NONE', #4021, #131028, #88585, .T. ) ;
#43589=LINE ( 'NONE', #142904, #82629 ) ;
#43591=CARTESIAN_POINT ( 'NONE',  ( -77.99451991528749772, 28.92564299267992567, 4.000000000000000000 ) ) ;
#43592=FACE_BOUND ( 'NONE', #128021, .T. ) ;
#43593=ORIENTED_EDGE ( 'NONE', *, *, #89660, .T. ) ;
#43594=EDGE_CURVE ( 'NONE', #68410, #65170, #43621, .T. ) ;
#43597=CARTESIAN_POINT ( 'NONE',  ( 0.005480084712502889671, 28.92564299267938210, 4.000000000000000000 ) ) ;
#43598=ORIENTED_EDGE ( 'NONE', *, *, #53196, .F. ) ;
#43600=ORIENTED_EDGE ( 'NONE', *, *, #136575, .F. ) ;
#43601=EDGE_LOOP ( 'NONE', ( #71905, #14008, #80422, #82995, #61269 ) ) ;
#43602=ORIENTED_EDGE ( 'NONE', *, *, #35920, .T. ) ;
#43604=EDGE_LOOP ( 'NONE', ( #62526, #121628, #80534, #10996, #73229, #51929 ) ) ;
#43605=AXIS2_PLACEMENT_3D ( 'NONE', #50232, #60409, #27029 ) ;
#43606=CARTESIAN_POINT ( 'NONE',  ( 27.18398860626900060, 28.73617430169806042, 5.000000000000000000 ) ) ;
#43607=CARTESIAN_POINT ( 'NONE',  ( -14.99451991528749595, 28.92564299267948513, 4.000000000000000000 ) ) ;
#43608=CARTESIAN_POINT ( 'NONE',  ( 69.48921356237309510, -27.52281430457103895, 5.000000000000000000 ) ) ;
#43609=ORIENTED_EDGE ( 'NONE', *, *, #49006, .T. ) ;
#43610=LINE ( 'NONE', #123344, #35311 ) ;
#43611=DIRECTION ( 'NONE',  ( 0.7071067811865486830, -0.7071067811865464625, -0.000000000000000000 ) ) ;
#43612=PLANE ( 'NONE',  #142751 ) ;
#43613=DIRECTION ( 'NONE',  ( -0.6830127018922180770, -0.6830127018922204085, -0.2588190451025213501 ) ) ;
#43614=FACE_OUTER_BOUND ( 'NONE', #126286, .T. ) ;
#43615=FACE_OUTER_BOUND ( 'NONE', #73674, .T. ) ;
#43616=CARTESIAN_POINT ( 'NONE',  ( 0.000000000000000000, 0.000000000000000000, 5.000000000000000000 ) ) ;
#43618=EDGE_CURVE ( 'NONE', #115783, #949, #100860, .T. ) ;
#43619=ORIENTED_EDGE ( 'NONE', *, *, #16119, .T. ) ;
#43621=LINE ( 'NONE', #46539, #17229 ) ;
#43622=VECTOR ( 'NONE', #7000, 999.9999999999998863 ) ;
#43623=VECTOR ( 'NONE', #141354, 1000.000000000000000 ) ;
#43624=CARTESIAN_POINT ( 'NONE',  ( 16.49999999999988987, -1.592773361805348342, -6.492772025301264627 ) ) ;
#43625=VERTEX_POINT ( 'NONE', #10269 ) ;
#43626=VECTOR ( 'NONE', #88549, 1000.000000000000000 ) ;
#43627=VERTEX_POINT ( 'NONE', #98709 ) ;
#43629=FACE_OUTER_BOUND ( 'NONE', #74810, .T. ) ;
#43630=VECTOR ( 'NONE', #111408, 1000.000000000000000 ) ;
#43631=EDGE_CURVE ( 'NONE', #2199, #96833, #55965, .T. ) ;
#43632=ADVANCED_FACE ( 'NONE', ( #66813 ), #76270, .F. ) ;
#43633=DIRECTION ( 'NONE',  ( 0.7071067811865487940, 0.7071067811865463515, 0.000000000000000000 ) ) ;
#43634=VERTEX_POINT ( 'NONE', #87846 ) ;
#43635=LINE ( 'NONE', #78416, #30125 ) ;
#43636=AXIS2_PLACEMENT_3D ( 'NONE', #114571, #124747, #124044 ) ;
#43637=VECTOR ( 'NONE', #121226, 1000.000000000000000 ) ;
#43638=DIRECTION ( 'NONE',  ( -0.6830127018922181881, 0.6830127018922202975, -0.2588190451025214056 ) ) ;
#43640=EDGE_CURVE ( 'NONE', #79902, #125706, #21870, .T. ) ;
#43642=PLANE ( 'NONE',  #32308 ) ;
#43644=ORIENTED_EDGE ( 'NONE', *, *, #5245, .T. ) ;
#43648=CARTESIAN_POINT ( 'NONE',  ( 26.53839644629413286, -9.740707523384177335, 17.74957260769616951 ) ) ;
#43649=DIRECTION ( 'NONE',  ( 0.7071067811865487940, 0.7071067811865463515, 0.000000000000000000 ) ) ;
#43650=ORIENTED_EDGE ( 'NONE', *, *, #134544, .T. ) ;
#43652=ORIENTED_EDGE ( 'NONE', *, *, #65123, .T. ) ;
#43653=ADVANCED_FACE ( 'NONE', ( #103683 ), #79875, .T. ) ;
#43654=CARTESIAN_POINT ( 'NONE',  ( 51.48921356237309510, -27.52281430457091460, 5.000000000000000000 ) ) ;
#43655=CARTESIAN_POINT ( 'NONE',  ( 38.99451991528749062, 28.92564299267965211, 4.000000000000000000 ) ) ;
#43657=VERTEX_POINT ( 'NONE', #102320 ) ;
#43658=EDGE_CURVE ( 'NONE', #92295, #133006, #47946, .T. ) ;
#43659=CARTESIAN_POINT ( 'NONE',  ( -11.20710678118646442, -8.240707523384198652, 5.000000000000000000 ) ) ;
#43660=CARTESIAN_POINT ( 'NONE',  ( 57.29974487139158157, -27.71228299555246011, 4.000000000000000000 ) ) ;
#43661=VERTEX_POINT ( 'NONE', #24724 ) ;
#43662=VECTOR ( 'NONE', #73147, 1000.000000000000000 ) ;
#43663=LINE ( 'NONE', #19056, #101795 ) ;
#43664=( BOUNDED_CURVE ( )  B_SPLINE_CURVE ( 3, ( #83884, #7694, #130224, #128089 ),
 .UNSPECIFIED., .F., .T. ) 
 B_SPLINE_CURVE_WITH_KNOTS ( ( 4, 4 ),
 ( 1.500914606003786567, 1.515984175831967429 ),
 .UNSPECIFIED. ) 
 CURVE ( )  GEOMETRIC_REPRESENTATION_ITEM ( )  RATIONAL_B_SPLINE_CURVE ( ( 1.000000000000000000, 0.9999810757616318657, 0.9999810757616318657, 1.000000000000000000 ) ) 
 REPRESENTATION_ITEM ( '' )  );
#43665=DIRECTION ( 'NONE',  ( 0.7071067811865486830, -0.7071067811865464625, -0.000000000000000000 ) ) ;
#43666=VECTOR ( 'NONE', #51362, 1000.000000000000000 ) ;
#43667=ORIENTED_EDGE ( 'NONE', *, *, #120606, .T. ) ;
#43668=ADVANCED_FACE ( 'NONE', ( #93562 ), #113145, .T. ) ;
#43670=CARTESIAN_POINT ( 'NONE',  ( 63.48921356237309510, -27.52281430457099631, 5.000000000000000000 ) ) ;
#43671=LINE ( 'NONE', #71152, #39400 ) ;
#43672=ORIENTED_EDGE ( 'NONE', *, *, #82601, .F. ) ;
#43673=EDGE_LOOP ( 'NONE', ( #63473, #49014, #105239, #79551, #129603, #45786 ) ) ;
#43674=DIRECTION ( 'NONE',  ( 0.7071067811865487940, 0.7071067811865463515, 0.000000000000000000 ) ) ;
#43675=AXIS2_PLACEMENT_3D ( 'NONE', #60863, #29594, #6373 ) ;
#43676=DIRECTION ( 'NONE',  ( 0.7071067811865487940, 0.7071067811865463515, 0.000000000000000000 ) ) ;
#43677=EDGE_CURVE ( 'NONE', #100225, #116904, #27561, .T. ) ;
#43678=ORIENTED_EDGE ( 'NONE', *, *, #346, .F. ) ;
#43680=DIRECTION ( 'NONE',  ( -1.000000000000000000, 0.000000000000000000, 0.000000000000000000 ) ) ;
#43681=LINE ( 'NONE', #77052, #5181 ) ;
#43683=DIRECTION ( 'NONE',  ( -0.7071067811865487940, 0.7071067811865463515, 0.000000000000000000 ) ) ;
#43684=DIRECTION ( 'NONE',  ( -0.000000000000000000, 0.3543493200069153248, 0.9351131265310292928 ) ) ;
#43688=CARTESIAN_POINT ( 'NONE',  ( 13.78302761116349728, -22.22500000000000142, 23.45729246355647746 ) ) ;
#43689=AXIS2_PLACEMENT_3D ( 'NONE', #73475, #6020, #96595 ) ;
#43690=VERTEX_POINT ( 'NONE', #135643 ) ;
#43691=ORIENTED_EDGE ( 'NONE', *, *, #128854, .F. ) ;
#43692=EDGE_CURVE ( 'NONE', #69387, #71257, #124753, .T. ) ;
#43694=ORIENTED_EDGE ( 'NONE', *, *, #43528, .T. ) ;
#43695=ADVANCED_FACE ( 'NONE', ( #115998 ), #26168, .F. ) ;
#43696=VERTEX_POINT ( 'NONE', #105142 ) ;
#43697=LINE ( 'NONE', #118384, #33986 ) ;
#43698=DIRECTION ( 'NONE',  ( -0.000000000000000000, 0.000000000000000000, 1.000000000000000000 ) ) ;
#43701=FACE_OUTER_BOUND ( 'NONE', #37169, .T. ) ;
#43702=CARTESIAN_POINT ( 'NONE',  ( 21.48921356237309155, -27.52281430457070499, 5.000000000000000000 ) ) ;
#43703=CARTESIAN_POINT ( 'NONE',  ( 4.499999999999972466, -2.947814304570806065, 5.000000000000000000 ) ) ;
#43704=CARTESIAN_POINT ( 'NONE',  ( 63.48921356237309510, -27.52281430457099631, 5.000000000000000000 ) ) ;
#43706=ORIENTED_EDGE ( 'NONE', *, *, #56184, .T. ) ;
#43707=LINE ( 'NONE', #108933, #85759 ) ;
#43709=LINE ( 'NONE', #121259, #68097 ) ;
#43710=LINE ( 'NONE', #108210, #114985 ) ;
#43711=CARTESIAN_POINT ( 'NONE',  ( 21.48921356237309155, -27.52281430457070499, 5.000000000000000000 ) ) ;
#43712=CARTESIAN_POINT ( 'NONE',  ( -42.18398860626899705, 28.73617430169816700, 5.000000000000000000 ) ) ;
#43713=CARTESIAN_POINT ( 'NONE',  ( 0.000000000000000000, 0.000000000000000000, 5.000000000000000000 ) ) ;
#43715=DIRECTION ( 'NONE',  ( -0.7071067811865486830, -0.7071067811865464625, 0.000000000000000000 ) ) ;
#43716=FACE_OUTER_BOUND ( 'NONE', #83555, .T. ) ;
#43717=EDGE_LOOP ( 'NONE', ( #99061, #58848, #110115, #86965 ) ) ;
#43718=ORIENTED_EDGE ( 'NONE', *, *, #122037, .F. ) ;
#43720=EDGE_CURVE ( 'NONE', #122494, #29125, #92110, .T. ) ;
#43721=CYLINDRICAL_SURFACE ( 'NONE', #71739, 0.5000000000000004441 ) ;
#43722=CARTESIAN_POINT ( 'NONE',  ( 60.48921356237309510, -27.52281430457097500, 5.000000000000000000 ) ) ;
#43723=ORIENTED_EDGE ( 'NONE', *, *, #23206, .T. ) ;
#43724=DIRECTION ( 'NONE',  ( 0.7071067811865487940, 0.7071067811865463515, 0.000000000000000000 ) ) ;
#43725=CARTESIAN_POINT ( 'NONE',  ( 66.48921356237309510, -27.52281430457101763, 5.000000000000000000 ) ) ;
#43727=EDGE_LOOP ( 'NONE', ( #15313, #48654, #87876, #5437 ) ) ;
#43728=ORIENTED_EDGE ( 'NONE', *, *, #120365, .T. ) ;
#43730=FACE_OUTER_BOUND ( 'NONE', #131024, .T. ) ;
#43731=VECTOR ( 'NONE', #66276, 1000.000000000000000 ) ;
#43732=AXIS2_PLACEMENT_3D ( 'NONE', #13498, #91791, #88971 ) ;
#43733=VECTOR ( 'NONE', #71077, 1000.000000000000000 ) ;
#43734=DIRECTION ( 'NONE',  ( -0.7071067811865486830, -0.7071067811865464625, -0.000000000000000000 ) ) ;
#43735=CARTESIAN_POINT ( 'NONE',  ( 38.99451991528749062, 28.92564299267965211, 4.000000000000000000 ) ) ;
#43736=VECTOR ( 'NONE', #36294, 1000.000000000000000 ) ;
#43737=CARTESIAN_POINT ( 'NONE',  ( -14.67183060077637080, -15.74070752338413115, 4.000000000000000000 ) ) ;
#43738=ORIENTED_EDGE ( 'NONE', *, *, #26899, .F. ) ;
#43742=PLANE ( 'NONE',  #96161 ) ;
#43743=ORIENTED_EDGE ( 'NONE', *, *, #139300, .F. ) ;
#43746=EDGE_CURVE ( 'NONE', #116279, #97308, #35647, .T. ) ;
#43747=FACE_OUTER_BOUND ( 'NONE', #142268, .T. ) ;
#43748=AXIS2_PLACEMENT_3D ( 'NONE', #142609, #75226, #119388 ) ;
#43750=CARTESIAN_POINT ( 'NONE',  ( 34.92499999999998295, 19.80009451602697013, 4.759050581649324485 ) ) ;
#43751=AXIS2_PLACEMENT_3D ( 'NONE', #66869, #111041, #20474 ) ;
#43752=ADVANCED_FACE ( 'NONE', ( #8633 ), #31172, .F. ) ;
#43753=ORIENTED_EDGE ( 'NONE', *, *, #77390, .F. ) ;
#43756=CARTESIAN_POINT ( 'NONE',  ( -34.92500000000001137, 9.856123077392346943, 4.000000000000000000 ) ) ;
#43757=CARTESIAN_POINT ( 'NONE',  ( 9.005480084712511157, 28.92564299267931816, 4.000000000000000000 ) ) ;
#43758=PLANE ( 'NONE',  #43245 ) ;
#43759=ORIENTED_EDGE ( 'NONE', *, *, #110966, .T. ) ;
#43760=ORIENTED_EDGE ( 'NONE', *, *, #109080, .F. ) ;
#43762=LINE ( 'NONE', #19152, #84067 ) ;
#43763=ORIENTED_EDGE ( 'NONE', *, *, #48362, .T. ) ;
#43765=ORIENTED_EDGE ( 'NONE', *, *, #57189, .T. ) ;
#43766=VECTOR ( 'NONE', #36570, 1000.000000000000000 ) ;
#43767=ADVANCED_FACE ( 'NONE', ( #96372 ), #62374, .F. ) ;
#43768=LINE ( 'NONE', #53199, #116185 ) ;
#43769=ORIENTED_EDGE ( 'NONE', *, *, #143215, .T. ) ;
#43770=DIRECTION ( 'NONE',  ( 0.7071067811865486830, -0.7071067811865464625, -0.000000000000000000 ) ) ;
#43771=CARTESIAN_POINT ( 'NONE',  ( 19.17183060077634593, 12.75929247661559529, 4.000000000000000000 ) ) ;
#43773=VECTOR ( 'NONE', #36557, 1000.000000000000000 ) ;
#43774=LINE ( 'NONE', #68417, #37348 ) ;
#43775=AXIS2_PLACEMENT_3D ( 'NONE', #23703, #101979, #122276 ) ;
#43776=FACE_BOUND ( 'NONE', #54160, .T. ) ;
#43777=EDGE_CURVE ( 'NONE', #78073, #42223, #139832, .T. ) ;
#43779=PLANE ( 'NONE',  #139263 ) ;
#43780=FACE_OUTER_BOUND ( 'NONE', #86971, .T. ) ;
#43782=VERTEX_POINT ( 'NONE', #127622 ) ;
#43783=AXIS2_PLACEMENT_3D ( 'NONE', #72998, #125919, #139673 ) ;
#43784=AXIS2_PLACEMENT_3D ( 'NONE', #27544, #48612, #5060 ) ;
#43787=VERTEX_POINT ( 'NONE', #73946 ) ;
#43788=ORIENTED_EDGE ( 'NONE', *, *, #93771, .T. ) ;
#43790=EDGE_LOOP ( 'NONE', ( #2356, #132845, #1538, #33686 ) ) ;
#43791=DIRECTION ( 'NONE',  ( -0.000000000000000000, -0.3543493200069152693, 0.9351131265310292928 ) ) ;
#43792=LINE ( 'NONE', #65582, #76786 ) ;
#43793=ORIENTED_EDGE ( 'NONE', *, *, #23235, .T. ) ;
#43794=FACE_OUTER_BOUND ( 'NONE', #60167, .T. ) ;
#43795=VECTOR ( 'NONE', #32819, 1000.000000000000227 ) ;
#43796=LINE ( 'NONE', #97434, #54252 ) ;
#43797=LINE ( 'NONE', #77855, #113146 ) ;
#43798=DIRECTION ( 'NONE',  ( 1.000000000000000000, 0.000000000000000000, 0.000000000000000000 ) ) ;
#43799=DIRECTION ( 'NONE',  ( -0.6830127018922180770, -0.6830127018922204085, -0.2588190451025213501 ) ) ;
#43800=LINE ( 'NONE', #88016, #49612 ) ;
#43801=CARTESIAN_POINT ( 'NONE',  ( -24.77004279457776548, 21.73644205237997795, 5.000000000000000000 ) ) ;
#43802=LINE ( 'NONE', #30802, #23096 ) ;
#43803=ADVANCED_FACE ( 'NONE', ( #139228 ), #30448, .F. ) ;
#43804=ORIENTED_EDGE ( 'NONE', *, *, #106867, .T. ) ;
#43805=DIRECTION ( 'NONE',  ( -0.7071067811865486830, -0.7071067811865464625, -0.000000000000000000 ) ) ;
#43806=ORIENTED_EDGE ( 'NONE', *, *, #111079, .T. ) ;
#43807=CARTESIAN_POINT ( 'NONE',  ( 51.29974487139158867, -27.71228299555242103, 4.000000000000000000 ) ) ;
#43808=PLANE ( 'NONE',  #72114 ) ;
#43811=CARTESIAN_POINT ( 'NONE',  ( 48.48921356237309510, -27.52281430457089328, 5.000000000000000000 ) ) ;
#43812=EDGE_CURVE ( 'NONE', #49913, #99410, #108668, .T. ) ;
#43813=CARTESIAN_POINT ( 'NONE',  ( -71.99451991528749772, 28.92564299267988304, 4.000000000000000000 ) ) ;
#43814=ORIENTED_EDGE ( 'NONE', *, *, #120353, .T. ) ;
#43815=LINE ( 'NONE', #67000, #46322 ) ;
#43821=ORIENTED_EDGE ( 'NONE', *, *, #53389, .F. ) ;
#43824=ORIENTED_EDGE ( 'NONE', *, *, #124068, .T. ) ;
#43826=DIRECTION ( 'NONE',  ( 0.7071067811865487940, 0.7071067811865463515, 0.000000000000000000 ) ) ;
#43827=ORIENTED_EDGE ( 'NONE', *, *, #1838, .T. ) ;
#43828=VERTEX_POINT ( 'NONE', #52185 ) ;
#43829=EDGE_CURVE ( 'NONE', #62423, #58035, #138498, .T. ) ;
#43830=DIRECTION ( 'NONE',  ( 0.7071067811865487940, 0.7071067811865463515, 0.000000000000000000 ) ) ;
#43831=DIRECTION ( 'NONE',  ( 0.7071067811865486830, -0.7071067811865464625, -0.000000000000000000 ) ) ;
#43832=CARTESIAN_POINT ( 'NONE',  ( 66.48921356237309510, -27.52281430457101763, 5.000000000000000000 ) ) ;
#43833=VERTEX_POINT ( 'NONE', #94960 ) ;
#43835=VERTEX_POINT ( 'NONE', #39181 ) ;
#43836=ORIENTED_EDGE ( 'NONE', *, *, #108431, .T. ) ;
#43837=EDGE_CURVE ( 'NONE', #86852, #142915, #19556, .T. ) ;
#43838=DIRECTION ( 'NONE',  ( -0.7071067811865487940, 0.7071067811865463515, -0.000000000000000000 ) ) ;
#43839=DIRECTION ( 'NONE',  ( -0.000000000000000000, -0.3543493200069152693, 0.9351131265310292928 ) ) ;
#43840=VECTOR ( 'NONE', #34141, 1000.000000000000227 ) ;
#43842=AXIS2_PLACEMENT_3D ( 'NONE', #36543, #34406, #69187 ) ;
#43843=VECTOR ( 'NONE', #95264, 1000.000000000000000 ) ;
#43844=FACE_OUTER_BOUND ( 'NONE', #60093, .T. ) ;
#43845=PLANE ( 'NONE',  #79403 ) ;
#43846=PLANE ( 'NONE',  #39910 ) ;
#43849=DIRECTION ( 'NONE',  ( -0.7071067811865486830, -0.7071067811865464625, 0.000000000000000000 ) ) ;
#43851=EDGE_CURVE ( 'NONE', #99565, #58487, #34028, .T. ) ;
#43852=ORIENTED_EDGE ( 'NONE', *, *, #127837, .T. ) ;
#43853=DIRECTION ( 'NONE',  ( 0.6830127018922180770, -0.6830127018922204085, -0.2588190451025214056 ) ) ;
#43854=ORIENTED_EDGE ( 'NONE', *, *, #126316, .T. ) ;
#43855=VECTOR ( 'NONE', #131232, 1000.000000000000000 ) ;
#43856=DIRECTION ( 'NONE',  ( -0.000000000000000000, -0.3543493200069152693, 0.9351131265310292928 ) ) ;
#43857=( BOUNDED_CURVE ( )  B_SPLINE_CURVE ( 3, ( #77768, #68351, #46613, #103083 ),
 .UNSPECIFIED., .F., .T. ) 
 B_SPLINE_CURVE_WITH_KNOTS ( ( 4, 4 ),
 ( 5.043186909253405403, 5.074607125596340751 ),
 .UNSPECIFIED. ) 
 CURVE ( )  GEOMETRIC_REPRESENTATION_ITEM ( )  RATIONAL_B_SPLINE_CURVE ( ( 1.000000000000000000, 0.9999177325257868620, 0.9999177325257868620, 1.000000000000000000 ) ) 
 REPRESENTATION_ITEM ( '' )  );
#43858=EDGE_CURVE ( 'NONE', #3663, #115089, #44941, .T. ) ;
#43859=CARTESIAN_POINT ( 'NONE',  ( 13.17183060077637968, 15.75929247661555443, 4.000000000000000000 ) ) ;
#43862=DIRECTION ( 'NONE',  ( -0.6830127018922180770, -0.6830127018922204085, -0.2588190451025213501 ) ) ;
#43863=DIRECTION ( 'NONE',  ( -0.7071067811865486830, -0.7071067811865464625, 0.000000000000000000 ) ) ;
#43864=CARTESIAN_POINT ( 'NONE',  ( -25.17183060077629619, -14.24070752338412937, 4.000000000000000000 ) ) ;
#43865=ORIENTED_EDGE ( 'NONE', *, *, #66637, .F. ) ;
#43866=ORIENTED_EDGE ( 'NONE', *, *, #134161, .F. ) ;
#43868=CARTESIAN_POINT ( 'NONE',  ( 18.48921356237309510, -27.52281430457068367, 5.000000000000000000 ) ) ;
#43869=CARTESIAN_POINT ( 'NONE',  ( -2.999999999999978240, -13.44781430457069327, 5.000000000000000000 ) ) ;
#43871=CARTESIAN_POINT ( 'NONE',  ( -7.828169399223474656, -11.24070752338416845, 4.000000000000000000 ) ) ;
#43872=CARTESIAN_POINT ( 'NONE',  ( 10.00193056682090642, -22.22500000000000142, 4.500000000000000888 ) ) ;
#43875=VECTOR ( 'NONE', #135733, 1000.000000000000000 ) ;
#43876=LINE ( 'NONE', #33027, #134129 ) ;
#43877=CARTESIAN_POINT ( 'NONE',  ( 6.299744871391586898, -27.71228299555210484, 4.000000000000000000 ) ) ;
#43878=DIRECTION ( 'NONE',  ( 0.7071067811865486830, 0.7071067811865464625, 0.000000000000000000 ) ) ;
#43879=VERTEX_POINT ( 'NONE', #131903 ) ;
#43880=EDGE_CURVE ( 'NONE', #67478, #21645, #120255, .T. ) ;
#43881=ORIENTED_EDGE ( 'NONE', *, *, #121071, .F. ) ;
#43882=DIRECTION ( 'NONE',  ( 0.7071067811865487940, 0.7071067811865463515, 0.000000000000000000 ) ) ;
#43883=DIRECTION ( 'NONE',  ( 0.7071067811865487940, 0.7071067811865463515, -0.000000000000000000 ) ) ;
#43884=VECTOR ( 'NONE', #69090, 999.9999999999998863 ) ;
#43885=VECTOR ( 'NONE', #106795, 1000.000000000000227 ) ;
#43886=VECTOR ( 'NONE', #137120, 1000.000000000000227 ) ;
#43887=PLANE ( 'NONE',  #20678 ) ;
#43888=CARTESIAN_POINT ( 'NONE',  ( -34.92500000000001137, 21.72500000000000142, 5.000000000000000000 ) ) ;
#43889=DIRECTION ( 'NONE',  ( 0.7071067811865487940, 0.7071067811865463515, 0.000000000000000000 ) ) ;
#43890=CARTESIAN_POINT ( 'NONE',  ( -11.81601139373100651, 28.73617430169779041, 5.000000000000000000 ) ) ;
#43891=LINE ( 'NONE', #9814, #7842 ) ;
#43892=ORIENTED_EDGE ( 'NONE', *, *, #126862, .F. ) ;
#43893=ORIENTED_EDGE ( 'NONE', *, *, #21944, .F. ) ;
#43895=FACE_OUTER_BOUND ( 'NONE', #1224, .T. ) ;
#43896=VECTOR ( 'NONE', #28580, 1000.000000000000000 ) ;
#43897=CARTESIAN_POINT ( 'NONE',  ( -13.17183060077638324, -17.24070752338410628, 4.000000000000000000 ) ) ;
#43898=ADVANCED_FACE ( 'NONE', ( #134049 ), #21706, .F. ) ;
#43899=CARTESIAN_POINT ( 'NONE',  ( 5.999999999999956479, -8.151047557385066256, -8.977947279169812944 ) ) ;
#43901=DIRECTION ( 'NONE',  ( 0.7071067811865487940, 0.7071067811865463515, 0.000000000000000000 ) ) ;
#43902=DIRECTION ( 'NONE',  ( -0.7071067811865487940, 0.7071067811865463515, 0.000000000000000000 ) ) ;
#43903=VERTEX_POINT ( 'NONE', #43459 ) ;
#43905=DIRECTION ( 'NONE',  ( -0.000000000000000000, 0.000000000000000000, 1.000000000000000000 ) ) ;
#43906=EDGE_CURVE ( 'NONE', #42897, #62746, #44191, .T. ) ;
#43907=DIRECTION ( 'NONE',  ( 0.7071067811865487940, 0.7071067811865463515, 0.000000000000000000 ) ) ;
#43908=FACE_OUTER_BOUND ( 'NONE', #102112, .T. ) ;
#43909=VECTOR ( 'NONE', #121671, 1000.000000000000000 ) ;
#43910=VERTEX_POINT ( 'NONE', #77543 ) ;
#43911=DIRECTION ( 'NONE',  ( -0.6830127018922181881, 0.6830127018922202975, -0.2588190451025214056 ) ) ;
#43913=EDGE_CURVE ( 'NONE', #63953, #75609, #34734, .T. ) ;
#43914=PLANE ( 'NONE',  #53540 ) ;
#43916=CARTESIAN_POINT ( 'NONE',  ( -2.816011393730999401, 28.73617430169785436, 5.000000000000000000 ) ) ;
#43918=DIRECTION ( 'NONE',  ( 0.7071067811865486830, -0.7071067811865464625, -0.000000000000000000 ) ) ;
#43919=LINE ( 'NONE', #51411, #110072 ) ;
#43920=CARTESIAN_POINT ( 'NONE',  ( -18.18398860626898994, 28.73617430169800002, 5.000000000000000000 ) ) ;
#43921=LINE ( 'NONE', #33080, #11437 ) ;
#43923=DIRECTION ( 'NONE',  ( -0.7071067811865487940, -0.7071067811865463515, -0.000000000000000000 ) ) ;
#43927=CARTESIAN_POINT ( 'NONE',  ( -36.48921356237310221, -27.52281430457080802, 5.000000000000000000 ) ) ;
#43929=LINE ( 'NONE', #77988, #41442 ) ;
#43930=ORIENTED_EDGE ( 'NONE', *, *, #113931, .T. ) ;
#43931=ORIENTED_EDGE ( 'NONE', *, *, #49249, .T. ) ;
#43933=ORIENTED_EDGE ( 'NONE', *, *, #9128, .F. ) ;
#43934=CARTESIAN_POINT ( 'NONE',  ( 22.49999999999984723, 18.05218569542898877, 5.000000000000000000 ) ) ;
#43935=DIRECTION ( 'NONE',  ( 0.7071067811865486830, -0.7071067811865464625, -0.000000000000000000 ) ) ;
#43937=ORIENTED_EDGE ( 'NONE', *, *, #56638, .F. ) ;
#43938=VERTEX_POINT ( 'NONE', #142769 ) ;
#43939=DIRECTION ( 'NONE',  ( -0.7071067811865487940, 0.7071067811865463515, -0.000000000000000000 ) ) ;
#43940=LINE ( 'NONE', #7712, #104568 ) ;
#43941=ORIENTED_EDGE ( 'NONE', *, *, #83255, .F. ) ;
#43942=EDGE_CURVE ( 'NONE', #97938, #97859, #31869, .T. ) ;
#43943=CARTESIAN_POINT ( 'NONE',  ( 12.79289321881337571, -2.240707523384255939, 5.000000000000000000 ) ) ;
#43944=CARTESIAN_POINT ( 'NONE',  ( -66.48921356237309510, -27.52281430457101763, 5.000000000000000000 ) ) ;
#43945=LINE ( 'NONE', #88170, #97919 ) ;
#43946=VECTOR ( 'NONE', #132823, 1000.000000000000000 ) ;
#43949=VERTEX_POINT ( 'NONE', #98544 ) ;
#43950=AXIS2_PLACEMENT_3D ( 'NONE', #61323, #27924, #96025 ) ;
#43951=EDGE_CURVE ( 'NONE', #111481, #110666, #11498, .T. ) ;
#43952=FACE_BOUND ( 'NONE', #93664, .T. ) ;
#43953=EDGE_CURVE ( 'NONE', #39036, #54633, #142083, .T. ) ;
#43954=CARTESIAN_POINT ( 'NONE',  ( -14.51078643762690490, -27.52281430457045275, 5.000000000000000000 ) ) ;
#43955=DIRECTION ( 'NONE',  ( -0.7071067811865487940, 0.7071067811865463515, -0.000000000000000000 ) ) ;
#43956=DIRECTION ( 'NONE',  ( 0.6830127018922181881, 0.6830127018922202975, -0.2588190451025214056 ) ) ;
#43957=VECTOR ( 'NONE', #105015, 1000.000000000000000 ) ;
#43958=DIRECTION ( 'NONE',  ( -0.7071067811865486830, -0.7071067811865464625, -0.000000000000000000 ) ) ;
#43961=ORIENTED_EDGE ( 'NONE', *, *, #95007, .T. ) ;
#43962=ORIENTED_EDGE ( 'NONE', *, *, #115960, .F. ) ;
#43964=ORIENTED_EDGE ( 'NONE', *, *, #6788, .T. ) ;
#43965=EDGE_LOOP ( 'NONE', ( #18515, #100743, #143426, #88936 ) ) ;
#43966=VECTOR ( 'NONE', #97153, 1000.000000000000000 ) ;
#43967=VECTOR ( 'NONE', #29606, 1000.000000000000000 ) ;
#43968=CARTESIAN_POINT ( 'NONE',  ( -21.29974487139158512, -27.71228299555221142, 4.000000000000000000 ) ) ;
#43969=EDGE_CURVE ( 'NONE', #78430, #141426, #67374, .T. ) ;
#43971=AXIS2_PLACEMENT_3D ( 'NONE', #137525, #59967, #127342 ) ;
#43972=CARTESIAN_POINT ( 'NONE',  ( -34.92500000000001137, 16.81783344222318632, 7.048977539241899848 ) ) ;
#43973=ORIENTED_EDGE ( 'NONE', *, *, #90756, .F. ) ;
#43974=DIRECTION ( 'NONE',  ( -0.6830127018922181881, 0.6830127018922202975, -0.2588190451025214056 ) ) ;
#43977=FACE_OUTER_BOUND ( 'NONE', #64064, .T. ) ;
#43978=PLANE ( 'NONE',  #64303 ) ;
#43982=ORIENTED_EDGE ( 'NONE', *, *, #10968, .T. ) ;
#43984=DIRECTION ( 'NONE',  ( -0.7071067811865486830, -0.7071067811865464625, -0.000000000000000000 ) ) ;
#43986=ORIENTED_EDGE ( 'NONE', *, *, #116947, .F. ) ;
#43987=ORIENTED_EDGE ( 'NONE', *, *, #142063, .F. ) ;
#43988=AXIS2_PLACEMENT_3D ( 'NONE', #56455, #47013, #13578 ) ;
#43989=ORIENTED_EDGE ( 'NONE', *, *, #56784, .F. ) ;
#43991=AXIS2_PLACEMENT_3D ( 'NONE', #81746, #10889, #103437 ) ;
#43992=ORIENTED_EDGE ( 'NONE', *, *, #17224, .F. ) ;
#43993=CARTESIAN_POINT ( 'NONE',  ( 25.49999999999983302, 13.46639925780212721, 5.000000000000000000 ) ) ;
#43994=ADVANCED_FACE ( 'NONE', ( #121008 ), #100705, .F. ) ;
#43995=DIRECTION ( 'NONE',  ( 0.7071067811865487940, -0.7071067811865463515, 0.000000000000000000 ) ) ;
#43997=LINE ( 'NONE', #52015, #109606 ) ;
#43999=EDGE_LOOP ( 'NONE', ( #125626, #116166, #69031, #67151 ) ) ;
#44000=CARTESIAN_POINT ( 'NONE',  ( -17.99999999999986855, -18.41253812416056945, 4.000000000000000000 ) ) ;
#44001=VECTOR ( 'NONE', #79237, 1000.000000000000227 ) ;
#44002=PLANE ( 'NONE',  #12276 ) ;
#44006=LINE ( 'NONE', #111376, #82190 ) ;
#44007=ORIENTED_EDGE ( 'NONE', *, *, #12795, .F. ) ;
#44010=EDGE_LOOP ( 'NONE', ( #86174, #24001, #112815, #33947 ) ) ;
#44011=EDGE_LOOP ( 'NONE', ( #103345, #30033, #84713, #53133 ) ) ;
#44013=ORIENTED_EDGE ( 'NONE', *, *, #131370, .F. ) ;
#44015=PLANE ( 'NONE',  #44630 ) ;
#44016=ADVANCED_FACE ( 'NONE', ( #112299 ), #20976, .F. ) ;
#44017=DIRECTION ( 'NONE',  ( 0.7071067811865487940, 0.7071067811865463515, -0.000000000000000000 ) ) ;
#44018=EDGE_CURVE ( 'NONE', #18115, #74547, #65240, .T. ) ;
#44019=ORIENTED_EDGE ( 'NONE', *, *, #76930, .T. ) ;
#44020=LINE ( 'NONE', #131030, #97482 ) ;
#44021=EDGE_LOOP ( 'NONE', ( #45730, #21044, #105349, #57866 ) ) ;
#44022=VECTOR ( 'NONE', #138198, 1000.000000000000000 ) ;
#44024=EDGE_CURVE ( 'NONE', #26437, #23833, #87676, .T. ) ;
#44026=FACE_OUTER_BOUND ( 'NONE', #65973, .T. ) ;
#44027=DIRECTION ( 'NONE',  ( -0.000000000000000000, 0.000000000000000000, 1.000000000000000000 ) ) ;
#44028=LINE ( 'NONE', #77397, #25797 ) ;
#44029=ORIENTED_EDGE ( 'NONE', *, *, #89079, .F. ) ;
#44030=ORIENTED_EDGE ( 'NONE', *, *, #39914, .T. ) ;
#44031=ORIENTED_EDGE ( 'NONE', *, *, #107002, .F. ) ;
#44032=CARTESIAN_POINT ( 'NONE',  ( 36.29974487139159578, -27.71228299555231445, 4.000000000000000000 ) ) ;
#44034=EDGE_CURVE ( 'NONE', #78816, #53035, #25996, .T. ) ;
#44035=CARTESIAN_POINT ( 'NONE',  ( -21.18398860626899349, 28.73617430169802134, 5.000000000000000000 ) ) ;
#44036=CARTESIAN_POINT ( 'NONE',  ( -34.49999999999975131, 19.08746187583904685, 4.000000000000000000 ) ) ;
#44037=VECTOR ( 'NONE', #3331, 1000.000000000000000 ) ;
#44038=CARTESIAN_POINT ( 'NONE',  ( -34.49999999999975131, -13.91253812416061031, 4.000000000000000000 ) ) ;
#44039=LINE ( 'NONE', #33196, #102764 ) ;
#44040=CARTESIAN_POINT ( 'NONE',  ( -5.999999999999958256, 7.931123077392102871, 4.000000000000000000 ) ) ;
#44042=VERTEX_POINT ( 'NONE', #113709 ) ;
#44043=DIRECTION ( 'NONE',  ( 0.6830127018922181881, 0.6830127018922202975, -0.2588190451025214056 ) ) ;
#44044=VECTOR ( 'NONE', #78525, 1000.000000000000000 ) ;
#44045=EDGE_CURVE ( 'NONE', #18266, #82873, #91949, .T. ) ;
#44046=ORIENTED_EDGE ( 'NONE', *, *, #38402, .F. ) ;
#44047=VECTOR ( 'NONE', #104238, 999.9999999999998863 ) ;
#44048=VECTOR ( 'NONE', #73992, 1000.000000000000000 ) ;
#44049=VECTOR ( 'NONE', #37054, 1000.000000000000000 ) ;
#44050=DIRECTION ( 'NONE',  ( 0.7071067811865487940, 0.7071067811865463515, -0.000000000000000000 ) ) ;
#44051=ORIENTED_EDGE ( 'NONE', *, *, #123131, .F. ) ;
#44052=AXIS2_PLACEMENT_3D ( 'NONE', #32034, #99399, #88580 ) ;
#44053=FACE_OUTER_BOUND ( 'NONE', #142612, .T. ) ;
#44054=EDGE_LOOP ( 'NONE', ( #74139, #39295, #69821 ) ) ;
#44055=DIRECTION ( 'NONE',  ( -0.7071067811865486830, -0.7071067811865464625, 0.000000000000000000 ) ) ;
#44056=EDGE_LOOP ( 'NONE', ( #29460, #106274, #115273, #89510 ) ) ;
#44058=EDGE_LOOP ( 'NONE', ( #55254, #118075, #16254, #95821 ) ) ;
#44059=FACE_OUTER_BOUND ( 'NONE', #134116, .T. ) ;
#44060=AXIS2_PLACEMENT_3D ( 'NONE', #38193, #82407, #136763 ) ;
#44066=CARTESIAN_POINT ( 'NONE',  ( -34.92500000000001137, 18.94777415420116995, 3.758136617891472131 ) ) ;
#44067=LINE ( 'NONE', #123785, #134776 ) ;
#44068=LINE ( 'NONE', #88289, #65813 ) ;
#44069=CARTESIAN_POINT ( 'NONE',  ( 12.29974487139158512, -27.71228299555214747, 4.000000000000000000 ) ) ;
#44073=CARTESIAN_POINT ( 'NONE',  ( -2.540161610502588374, 18.75929247661552779, 8.305906642995479316 ) ) ;
#44074=CARTESIAN_POINT ( 'NONE',  ( -34.42500000000001137, 0.000000000000000000, 4.500000000000000888 ) ) ;
#44075=VERTEX_POINT ( 'NONE', #36853 ) ;
#44076=( BOUNDED_CURVE ( )  B_SPLINE_CURVE ( 3, ( #101311, #57841, #133254, #23760 ),
 .UNSPECIFIED., .F., .F. ) 
 B_SPLINE_CURVE_WITH_KNOTS ( ( 4, 4 ),
 ( 1.901594255663599853, 1.933014472006561624 ),
 .UNSPECIFIED. ) 
 CURVE ( )  GEOMETRIC_REPRESENTATION_ITEM ( )  RATIONAL_B_SPLINE_CURVE ( ( 1.000000000000000000, 0.9999177325257867510, 0.9999177325257867510, 1.000000000000000000 ) ) 
 REPRESENTATION_ITEM ( '' )  );
#44077=EDGE_LOOP ( 'NONE', ( #70047, #29655, #49563, #60402 ) ) ;
#44079=CARTESIAN_POINT ( 'NONE',  ( -12.79289321881337038, -2.240707523384259492, 5.000000000000000000 ) ) ;
#44081=VECTOR ( 'NONE', #10252, 1000.000000000000000 ) ;
#44082=EDGE_CURVE ( 'NONE', #78195, #27223, #3488, .T. ) ;
#44084=DIRECTION ( 'NONE',  ( -0.7071067811865487940, 0.7071067811865463515, 0.000000000000000000 ) ) ;
#44085=LINE ( 'NONE', #8533, #37018 ) ;
#44086=CARTESIAN_POINT ( 'NONE',  ( 9.183988606268997046, 28.73617430169793607, 5.000000000000000000 ) ) ;
#44087=CARTESIAN_POINT ( 'NONE',  ( 34.47516574401891631, 21.02806734111559450, 4.998110765256834398 ) ) ;
#44088=ORIENTED_EDGE ( 'NONE', *, *, #139427, .F. ) ;
#44089=VECTOR ( 'NONE', #21403, 999.9999999999998863 ) ;
#44090=DIRECTION ( 'NONE',  ( -0.7071067811865486830, -0.7071067811865464625, 0.000000000000000000 ) ) ;
#44091=CARTESIAN_POINT ( 'NONE',  ( 0.000000000000000000, -10.06887692260771416, 4.000000000000000000 ) ) ;
#44092=PLANE ( 'NONE',  #113573 ) ;
#44094=EDGE_CURVE ( 'NONE', #119104, #105661, #57942, .T. ) ;
#44095=VECTOR ( 'NONE', #75785, 999.9999999999998863 ) ;
#44096=LINE ( 'NONE', #122327, #44868 ) ;
#44097=LINE ( 'NONE', #141992, #130790 ) ;
#44098=ORIENTED_EDGE ( 'NONE', *, *, #82165, .F. ) ;
#44100=DIRECTION ( 'NONE',  ( 0.7071067811865486830, -0.7071067811865464625, -0.000000000000000000 ) ) ;
#44102=CARTESIAN_POINT ( 'NONE',  ( 9.083148067729251096, 21.75929247661549226, 7.311836541448074378 ) ) ;
#44103=DIRECTION ( 'NONE',  ( 0.6830127018922181881, 0.6830127018922202975, -0.2588190451025214056 ) ) ;
#44104=ORIENTED_EDGE ( 'NONE', *, *, #135695, .T. ) ;
#44105=ORIENTED_EDGE ( 'NONE', *, *, #60846, .F. ) ;
#44106=ORIENTED_EDGE ( 'NONE', *, *, #62543, .F. ) ;
#44109=ORIENTED_EDGE ( 'NONE', *, *, #110362, .F. ) ;
#44113=VERTEX_POINT ( 'NONE', #90545 ) ;
#44114=DIRECTION ( 'NONE',  ( -0.000000000000000000, 0.3543493200069153248, 0.9351131265310292928 ) ) ;
#44115=DIRECTION ( 'NONE',  ( -0.000000000000000000, -0.3543493200069152693, 0.9351131265310292928 ) ) ;
#44117=ORIENTED_EDGE ( 'NONE', *, *, #60220, .T. ) ;
#44118=EDGE_CURVE ( 'NONE', #130915, #125898, #24553, .T. ) ;
#44121=VECTOR ( 'NONE', #104424, 1000.000000000000000 ) ;
#44122=ORIENTED_EDGE ( 'NONE', *, *, #114054, .T. ) ;
#44123=ORIENTED_EDGE ( 'NONE', *, *, #53732, .T. ) ;
#44124=EDGE_CURVE ( 'NONE', #17758, #18398, #136891, .T. ) ;
#44125=ORIENTED_EDGE ( 'NONE', *, *, #19660, .T. ) ;
#44126=CARTESIAN_POINT ( 'NONE',  ( -30.18398860626900060, 28.73617430169808173, 5.000000000000000000 ) ) ;
#44127=ADVANCED_FACE ( 'NONE', ( #102850 ), #47781, .F. ) ;
#44130=LINE ( 'NONE', #7361, #58152 ) ;
#44131=VECTOR ( 'NONE', #71351, 1000.000000000000227 ) ;
#44133=LINE ( 'NONE', #98495, #62708 ) ;
#44134=DIRECTION ( 'NONE',  ( -0.3543493200069163240, 0.000000000000000000, -0.9351131265310288487 ) ) ;
#44135=VERTEX_POINT ( 'NONE', #36167 ) ;
#44137=EDGE_LOOP ( 'NONE', ( #127206, #33808, #118102, #8674 ) ) ;
#44138=CARTESIAN_POINT ( 'NONE',  ( 0.000000000000000000, 0.000000000000000000, 5.000000000000000000 ) ) ;
#44139=ORIENTED_EDGE ( 'NONE', *, *, #96509, .F. ) ;
#44140=ORIENTED_EDGE ( 'NONE', *, *, #142102, .F. ) ;
#44141=VECTOR ( 'NONE', #42925, 1000.000000000000000 ) ;
#44143=VECTOR ( 'NONE', #94543, 1000.000000000000000 ) ;
#44144=FACE_OUTER_BOUND ( 'NONE', #26189, .T. ) ;
#44145=ORIENTED_EDGE ( 'NONE', *, *, #70019, .T. ) ;
#44148=FACE_OUTER_BOUND ( 'NONE', #109438, .T. ) ;
#44149=CARTESIAN_POINT ( 'NONE',  ( 24.84463820744543838, 1.742823668393624903, 4.000000000000000000 ) ) ;
#44151=AXIS2_PLACEMENT_3D ( 'NONE', #117830, #71518, #73654 ) ;
#44152=AXIS2_PLACEMENT_3D ( 'NONE', #1890, #109984, #10650 ) ;
#44157=PLANE ( 'NONE',  #18640 ) ;
#44158=EDGE_LOOP ( 'NONE', ( #47018, #122745, #122258, #24504 ) ) ;
#44160=ORIENTED_EDGE ( 'NONE', *, *, #4077, .F. ) ;
#44161=CARTESIAN_POINT ( 'NONE',  ( 27.18398860626900060, 28.73617430169806042, 5.000000000000000000 ) ) ;
#44162=VERTEX_POINT ( 'NONE', #124587 ) ;
#44163=DIRECTION ( 'NONE',  ( 0.6830127018922180770, -0.6830127018922204085, -0.2588190451025213501 ) ) ;
#44164=VERTEX_POINT ( 'NONE', #70262 ) ;
#44168=ORIENTED_EDGE ( 'NONE', *, *, #46487, .F. ) ;
#44169=FACE_OUTER_BOUND ( 'NONE', #67714, .T. ) ;
#44170=EDGE_CURVE ( 'NONE', #65084, #50417, #26702, .T. ) ;
#44172=LINE ( 'NONE', #131886, #75046 ) ;
#44174=FACE_OUTER_BOUND ( 'NONE', #42127, .T. ) ;
#44175=EDGE_CURVE ( 'NONE', #121970, #19406, #125307, .T. ) ;
#44176=LINE ( 'NONE', #142070, #45988 ) ;
#44177=CARTESIAN_POINT ( 'NONE',  ( -30.48921356237309510, -27.52281430457076894, 5.000000000000000000 ) ) ;
#44178=CARTESIAN_POINT ( 'NONE',  ( 51.29974487139158867, -27.71228299555242103, 4.000000000000000000 ) ) ;
#44181=EDGE_CURVE ( 'NONE', #133096, #48518, #137621, .T. ) ;
#44182=EDGE_CURVE ( 'NONE', #71067, #115114, #27389, .T. ) ;
#44183=AXIS2_PLACEMENT_3D ( 'NONE', #86921, #119502, #41995 ) ;
#44184=VECTOR ( 'NONE', #104339, 1000.000000000000000 ) ;
#44185=CARTESIAN_POINT ( 'NONE',  ( 19.05000000000000071, 3.174999999999997158, 1.444000000000000394 ) ) ;
#44187=VERTEX_POINT ( 'NONE', #104230 ) ;
#44188=VECTOR ( 'NONE', #56048, 1000.000000000000227 ) ;
#44189=ORIENTED_EDGE ( 'NONE', *, *, #139454, .T. ) ;
#44191=LINE ( 'NONE', #23091, #121268 ) ;
#44192=EDGE_LOOP ( 'NONE', ( #82535, #49373, #41712, #41260 ) ) ;
#44193=AXIS2_PLACEMENT_3D ( 'NONE', #126939, #47999, #71897 ) ;
#44195=ORIENTED_EDGE ( 'NONE', *, *, #1868, .T. ) ;
#44196=DIRECTION ( 'NONE',  ( 0.7071067811865487940, 0.7071067811865463515, -0.000000000000000000 ) ) ;
#44198=EDGE_CURVE ( 'NONE', #120928, #128903, #79713, .T. ) ;
#44200=DIRECTION ( 'NONE',  ( -0.7071067811865487940, 0.7071067811865463515, -0.000000000000000000 ) ) ;
#44201=EDGE_CURVE ( 'NONE', #92353, #17336, #91274, .T. ) ;
#44202=FACE_OUTER_BOUND ( 'NONE', #29836, .T. ) ;
#44203=EDGE_LOOP ( 'NONE', ( #15604, #6101, #74907, #107004 ) ) ;
#44204=DIRECTION ( 'NONE',  ( -0.7071067811865487940, 0.7071067811865463515, -0.000000000000000000 ) ) ;
#44205=ORIENTED_EDGE ( 'NONE', *, *, #22020, .F. ) ;
#44206=CARTESIAN_POINT ( 'NONE',  ( 12.48921356237309155, -27.52281430457064104, 5.000000000000000000 ) ) ;
#44207=ADVANCED_FACE ( 'NONE', ( #75754 ), #143134, .F. ) ;
#44208=AXIS2_PLACEMENT_3D ( 'NONE', #135872, #14798, #59072 ) ;
#44210=ORIENTED_EDGE ( 'NONE', *, *, #74189, .F. ) ;
#44212=EDGE_CURVE ( 'NONE', #116810, #23874, #54720, .T. ) ;
#44214=DIRECTION ( 'NONE',  ( -0.6830127018922181881, 0.6830127018922202975, -0.2588190451025214056 ) ) ;
#44215=VERTEX_POINT ( 'NONE', #109062 ) ;
#44216=EDGE_LOOP ( 'NONE', ( #32599, #67418, #136472, #123959 ) ) ;
#44217=VECTOR ( 'NONE', #11404, 1000.000000000000227 ) ;
#44218=EDGE_LOOP ( 'NONE', ( #31962, #124733, #38449, #88182 ) ) ;
#44219=DIRECTION ( 'NONE',  ( 0.6830127018922181881, 0.6830127018922202975, -0.2588190451025214056 ) ) ;
#44220=LINE ( 'NONE', #2072, #57946 ) ;
#44221=CARTESIAN_POINT ( 'NONE',  ( -18.48921356237309510, -27.52281430457068367, 5.000000000000000000 ) ) ;
#44222=EDGE_CURVE ( 'NONE', #125554, #1609, #138322, .T. ) ;
#44223=CARTESIAN_POINT ( 'NONE',  ( 24.18398860626899705, 28.73617430169804265, 5.000000000000000000 ) ) ;
#44224=LINE ( 'NONE', #112323, #102846 ) ;
#44225=ORIENTED_EDGE ( 'NONE', *, *, #61419, .F. ) ;
#44227=CARTESIAN_POINT ( 'NONE',  ( 0.000000000000000000, -0.2811185226894302724, -5.995736974527512864 ) ) ;
#44228=FACE_OUTER_BOUND ( 'NONE', #129567, .T. ) ;
#44229=ORIENTED_EDGE ( 'NONE', *, *, #29763, .T. ) ;
#44230=CARTESIAN_POINT ( 'NONE',  ( -14.81601139373099585, 28.73617430169776910, 5.000000000000000000 ) ) ;
#44231=EDGE_CURVE ( 'NONE', #65716, #11235, #98900, .T. ) ;
#44232=AXIS2_PLACEMENT_3D ( 'NONE', #75930, #33178, #44775 ) ;
#44233=LINE ( 'NONE', #121046, #116458 ) ;
#44234=VERTEX_POINT ( 'NONE', #28134 ) ;
#44235=CARTESIAN_POINT ( 'NONE',  ( -23.33153258840129496, -18.74070752338409207, 20.73178291233835679 ) ) ;
#44236=ORIENTED_EDGE ( 'NONE', *, *, #58518, .F. ) ;
#44237=ORIENTED_EDGE ( 'NONE', *, *, #34108, .T. ) ;
#44238=FACE_OUTER_BOUND ( 'NONE', #36419, .T. ) ;
#44239=CARTESIAN_POINT ( 'NONE',  ( 34.49999999999975131, -20.94567065516883630, 4.994342998332155226 ) ) ;
#44240=EDGE_CURVE ( 'NONE', #121031, #34714, #54019, .T. ) ;
#44241=VECTOR ( 'NONE', #110554, 1000.000000000000227 ) ;
#44242=ORIENTED_EDGE ( 'NONE', *, *, #46676, .T. ) ;
#44243=CARTESIAN_POINT ( 'NONE',  ( -31.49999999999977973, -12.66682484999668823, -0.6294897503864678168 ) ) ;
#44244=DIRECTION ( 'NONE',  ( 0.6830127018922181881, 0.6830127018922202975, -0.2588190451025214056 ) ) ;
#44245=EDGE_CURVE ( 'NONE', #132249, #137138, #120645, .T. ) ;
#44247=( BOUNDED_CURVE ( )  B_SPLINE_CURVE ( 3, ( #14315, #70183, #81025, #16430 ),
 .UNSPECIFIED., .F., .T. ) 
 B_SPLINE_CURVE_WITH_KNOTS ( ( 4, 4 ),
 ( 1.378368140454908408, 1.408685637663195545 ),
 .UNSPECIFIED. ) 
 CURVE ( )  GEOMETRIC_REPRESENTATION_ITEM ( )  RATIONAL_B_SPLINE_CURVE ( ( 1.000000000000000000, 0.9999234055803066790, 0.9999234055803066790, 1.000000000000000000 ) ) 
 REPRESENTATION_ITEM ( '' )  );
#44248=DIRECTION ( 'NONE',  ( -0.6830127018922181881, 0.6830127018922202975, -0.2588190451025214056 ) ) ;
#44249=CARTESIAN_POINT ( 'NONE',  ( 34.42499999999998295, 22.22500000000000142, 0.4999999999999995559 ) ) ;
#44250=CARTESIAN_POINT ( 'NONE',  ( 51.18398860626899705, 28.73617430169823095, 5.000000000000000000 ) ) ;
#44251=DIRECTION ( 'NONE',  ( -1.000000000000000000, -6.248375730189539568E-15, 0.000000000000000000 ) ) ;
#44253=DIRECTION ( 'NONE',  ( -0.000000000000000000, 1.000000000000000000, -0.000000000000000000 ) ) ;
#44254=LINE ( 'NONE', #121771, #15881 ) ;
#44256=EDGE_CURVE ( 'NONE', #32728, #124559, #119920, .T. ) ;
#44257=CARTESIAN_POINT ( 'NONE',  ( -27.18398860626900060, 28.73617430169806042, 5.000000000000000000 ) ) ;
#44258=CARTESIAN_POINT ( 'NONE',  ( -23.59118151920504403, -0.6989376001503790903, 4.102600482792084335 ) ) ;
#44260=ORIENTED_EDGE ( 'NONE', *, *, #18257, .T. ) ;
#44261=VECTOR ( 'NONE', #38973, 1000.000000000000000 ) ;
#44265=VERTEX_POINT ( 'NONE', #76476 ) ;
#44266=VERTEX_POINT ( 'NONE', #97472 ) ;
#44267=DIRECTION ( 'NONE',  ( 2.781805975412905274E-17, -0.3543493200069152138, 0.9351131265310292928 ) ) ;
#44269=VECTOR ( 'NONE', #104263, 1000.000000000000000 ) ;
#44270=VECTOR ( 'NONE', #2474, 1000.000000000000000 ) ;
#44273=EDGE_LOOP ( 'NONE', ( #134590, #55409, #78117, #22180 ) ) ;
#44274=DIRECTION ( 'NONE',  ( -0.7071067811865486830, -0.7071067811865464625, -0.000000000000000000 ) ) ;
#44275=VECTOR ( 'NONE', #42245, 1000.000000000000000 ) ;
#44276=DIRECTION ( 'NONE',  ( -0.7071067811865486830, 0.7071067811865464625, 0.000000000000000000 ) ) ;
#44277=DIRECTION ( 'NONE',  ( 0.7071067811865487940, 0.7071067811865463515, -0.000000000000000000 ) ) ;
#44278=PLANE ( 'NONE',  #95224 ) ;
#44279=VERTEX_POINT ( 'NONE', #141726 ) ;
#44280=DIRECTION ( 'NONE',  ( 0.6830127018922180770, -0.6830127018922204085, -0.2588190451025213501 ) ) ;
#44281=CARTESIAN_POINT ( 'NONE',  ( -9.489213562373095101, -27.52281430457062328, 5.000000000000000000 ) ) ;
#44282=VECTOR ( 'NONE', #3399, 999.9999999999998863 ) ;
#44283=DIRECTION ( 'NONE',  ( -0.000000000000000000, 0.3543493200069153248, 0.9351131265310292928 ) ) ;
#44284=CARTESIAN_POINT ( 'NONE',  ( 25.49999999999983658, 13.56627193232217898, -10.57019076586062845 ) ) ;
#44285=LINE ( 'NONE', #133424, #88625 ) ;
#44286=LINE ( 'NONE', #129841, #36126 ) ;
#44287=CARTESIAN_POINT ( 'NONE',  ( 27.48921356237309155, -27.52281430457074762, 5.000000000000000000 ) ) ;
#44289=ORIENTED_EDGE ( 'NONE', *, *, #65798, .F. ) ;
#44290=ORIENTED_EDGE ( 'NONE', *, *, #11872, .T. ) ;
#44292=VERTEX_POINT ( 'NONE', #28851 ) ;
#44293=VECTOR ( 'NONE', #17720, 1000.000000000000000 ) ;
#44294=ADVANCED_FACE ( 'NONE', ( #116565 ), #131554, .F. ) ;
#44295=CARTESIAN_POINT ( 'NONE',  ( 10.49999999999992717, -10.53360074219763298, 5.000000000000000000 ) ) ;
#44296=FACE_OUTER_BOUND ( 'NONE', #47236, .T. ) ;
#44297=LINE ( 'NONE', #87068, #14282 ) ;
#44298=LINE ( 'NONE', #88512, #111285 ) ;
#44299=VECTOR ( 'NONE', #18409, 1000.000000000000000 ) ;
#44300=VECTOR ( 'NONE', #30193, 999.9999999999998863 ) ;
#44302=VERTEX_POINT ( 'NONE', #32239 ) ;
#44303=AXIS2_PLACEMENT_3D ( 'NONE', #91256, #69501, #68789 ) ;
#44304=ORIENTED_EDGE ( 'NONE', *, *, #8731, .F. ) ;
#44305=DIRECTION ( 'NONE',  ( 0.7071067811865487940, -0.7071067811865463515, 0.000000000000000000 ) ) ;
#44309=ORIENTED_EDGE ( 'NONE', *, *, #4287, .T. ) ;
#44312=ORIENTED_EDGE ( 'NONE', *, *, #6803, .T. ) ;
#44313=VECTOR ( 'NONE', #39244, 999.9999999999998863 ) ;
#44314=DIRECTION ( 'NONE',  ( 0.7071067811865487940, 0.7071067811865463515, -0.000000000000000000 ) ) ;
#44318=ADVANCED_FACE ( 'NONE', ( #61511 ), #86638, .F. ) ;
#44322=EDGE_CURVE ( 'NONE', #71223, #83238, #17925, .T. ) ;
#44323=CARTESIAN_POINT ( 'NONE',  ( -12.06039522340302028, -22.22500000000000142, -3.664253473662678839 ) ) ;
#44324=VERTEX_POINT ( 'NONE', #113342 ) ;
#44325=ORIENTED_EDGE ( 'NONE', *, *, #136392, .T. ) ;
#44326=VECTOR ( 'NONE', #115367, 1000.000000000000000 ) ;
#44328=VECTOR ( 'NONE', #69375, 1000.000000000000000 ) ;
#44329=EDGE_CURVE ( 'NONE', #123070, #68539, #14027, .T. ) ;
#44332=ORIENTED_EDGE ( 'NONE', *, *, #12714, .F. ) ;
#44333=LINE ( 'NONE', #131317, #117785 ) ;
#44334=AXIS2_PLACEMENT_3D ( 'NONE', #8545, #20161, #84731 ) ;
#44337=EDGE_CURVE ( 'NONE', #105294, #87228, #79361, .T. ) ;
#44338=FACE_OUTER_BOUND ( 'NONE', #110399, .T. ) ;
#44339=FACE_BOUND ( 'NONE', #58720, .T. ) ;
#44340=ORIENTED_EDGE ( 'NONE', *, *, #119085, .F. ) ;
#44342=CARTESIAN_POINT ( 'NONE',  ( 63.48921356237309510, -27.52281430457099631, 5.000000000000000000 ) ) ;
#44343=DIRECTION ( 'NONE',  ( -0.7071067811865486830, -0.7071067811865464625, 0.000000000000000000 ) ) ;
#44345=DIRECTION ( 'NONE',  ( 0.7071067811865486830, -0.7071067811865464625, -0.000000000000000000 ) ) ;
#44346=ORIENTED_EDGE ( 'NONE', *, *, #57982, .T. ) ;
#44347=EDGE_CURVE ( 'NONE', #132741, #3971, #101767, .T. ) ;
#44348=ORIENTED_EDGE ( 'NONE', *, *, #46480, .T. ) ;
#44349=VECTOR ( 'NONE', #125761, 999.9999999999998863 ) ;
#44350=DIRECTION ( 'NONE',  ( -0.000000000000000000, 0.000000000000000000, 1.000000000000000000 ) ) ;
#44351=VERTEX_POINT ( 'NONE', #55426 ) ;
#44353=EDGE_LOOP ( 'NONE', ( #45370, #40333, #66355, #101145 ) ) ;
#44354=CARTESIAN_POINT ( 'NONE',  ( -84.48921356237309510, -27.52281430457114197, 5.000000000000000000 ) ) ;
#44356=LINE ( 'NONE', #55212, #2386 ) ;
#44357=EDGE_CURVE ( 'NONE', #110443, #58071, #68470, .T. ) ;
#44358=EDGE_LOOP ( 'NONE', ( #114048, #51872, #33364, #39437 ) ) ;
#44359=DIRECTION ( 'NONE',  ( 0.7071067811865487940, 0.7071067811865463515, -0.000000000000000000 ) ) ;
#44360=CARTESIAN_POINT ( 'NONE',  ( 24.00548008471250938, 28.92564299267921513, 4.000000000000000000 ) ) ;
#44361=AXIS2_PLACEMENT_3D ( 'NONE', #13499, #46931, #100552 ) ;
#44363=AXIS2_PLACEMENT_3D ( 'NONE', #129930, #61839, #128511 ) ;
#44365=VECTOR ( 'NONE', #28637, 1000.000000000000227 ) ;
#44367=CARTESIAN_POINT ( 'NONE',  ( -3.489213562373097322, -27.52281430457057709, 5.000000000000000000 ) ) ;
#44369=FACE_OUTER_BOUND ( 'NONE', #108667, .T. ) ;
#44370=DIRECTION ( 'NONE',  ( 0.7071067811865486830, -0.7071067811865464625, -0.000000000000000000 ) ) ;
#44371=ORIENTED_EDGE ( 'NONE', *, *, #30022, .F. ) ;
#44372=AXIS2_PLACEMENT_3D ( 'NONE', #58539, #57794, #114283 ) ;
#44375=VECTOR ( 'NONE', #136936, 1000.000000000000000 ) ;
#44376=ORIENTED_EDGE ( 'NONE', *, *, #14160, .F. ) ;
#44377=AXIS2_PLACEMENT_3D ( 'NONE', #21473, #43237, #8400 ) ;
#44378=PLANE ( 'NONE',  #61273 ) ;
#44379=LINE ( 'NONE', #66119, #130137 ) ;
#44380=ORIENTED_EDGE ( 'NONE', *, *, #59584, .T. ) ;
#44381=EDGE_CURVE ( 'NONE', #77421, #121710, #13311, .T. ) ;
#44382=EDGE_LOOP ( 'NONE', ( #64167, #55060, #77339, #39073 ) ) ;
#44384=DIRECTION ( 'NONE',  ( -0.7071067811865486830, -0.7071067811865464625, -0.000000000000000000 ) ) ;
#44385=EDGE_CURVE ( 'NONE', #98086, #24434, #69163, .T. ) ;
#44386=FACE_OUTER_BOUND ( 'NONE', #105760, .T. ) ;
#44387=VERTEX_POINT ( 'NONE', #135151 ) ;
#44389=FACE_OUTER_BOUND ( 'NONE', #15128, .T. ) ;
#44390=FACE_OUTER_BOUND ( 'NONE', #111314, .T. ) ;
#44392=LINE ( 'NONE', #121891, #87859 ) ;
#44393=EDGE_LOOP ( 'NONE', ( #26955, #98469, #64935, #16054 ) ) ;
#44395=VECTOR ( 'NONE', #75017, 1000.000000000000000 ) ;
#44396=EDGE_CURVE ( 'NONE', #116339, #103515, #91614, .T. ) ;
#44397=LINE ( 'NONE', #142271, #92872 ) ;
#44398=CARTESIAN_POINT ( 'NONE',  ( -16.82816939922341959, -17.24070752338410983, 4.000000000000000000 ) ) ;
#44399=CARTESIAN_POINT ( 'NONE',  ( -60.18398860626900415, 28.73617430169829490, 5.000000000000000000 ) ) ;
#44401=CARTESIAN_POINT ( 'NONE',  ( -29.99999999999977973, 14.58746187583909126, 4.000000000000000000 ) ) ;
#44402=ORIENTED_EDGE ( 'NONE', *, *, #123134, .T. ) ;
#44403=DIRECTION ( 'NONE',  ( -0.7071067811865486830, -0.7071067811865464625, -0.000000000000000000 ) ) ;
#44404=CARTESIAN_POINT ( 'NONE',  ( -27.48921356237309155, -27.52281430457074762, 5.000000000000000000 ) ) ;
#44405=ADVANCED_FACE ( 'NONE', ( #124239 ), #24916, .F. ) ;
#44406=CARTESIAN_POINT ( 'NONE',  ( -53.99451991528749062, 28.92564299267975869, 4.000000000000000000 ) ) ;
#44407=LINE ( 'NONE', #124082, #132876 ) ;
#44408=ORIENTED_EDGE ( 'NONE', *, *, #10926, .T. ) ;
#44411=LINE ( 'NONE', #123396, #51090 ) ;
#44412=CARTESIAN_POINT ( 'NONE',  ( -37.06996025486385093, -0.7407075233842735917, 13.87443053587619701 ) ) ;
#44413=ORIENTED_EDGE ( 'NONE', *, *, #126582, .F. ) ;
#44414=LINE ( 'NONE', #75593, #127237 ) ;
#44415=VECTOR ( 'NONE', #7105, 1000.000000000000000 ) ;
#44416=DIRECTION ( 'NONE',  ( 0.7071067811865487940, 0.7071067811865463515, -0.000000000000000000 ) ) ;
#44418=CARTESIAN_POINT ( 'NONE',  ( -5.999999999999958256, 2.966399257802234235, 5.000000000000000000 ) ) ;
#44419=CARTESIAN_POINT ( 'NONE',  ( -2.816011393730999401, 28.73617430169785436, 5.000000000000000000 ) ) ;
#44420=ORIENTED_EDGE ( 'NONE', *, *, #37070, .F. ) ;
#44423=CARTESIAN_POINT ( 'NONE',  ( 31.49999999999978684, 18.05218569542898521, 5.000000000000000000 ) ) ;
#44424=VECTOR ( 'NONE', #76435, 1000.000000000000000 ) ;
#44425=VERTEX_POINT ( 'NONE', #11150 ) ;
#44427=ADVANCED_FACE ( 'NONE', ( #285 ), #100357, .F. ) ;
#44428=FACE_OUTER_BOUND ( 'NONE', #51800, .T. ) ;
#44430=ORIENTED_EDGE ( 'NONE', *, *, #14729, .F. ) ;
#44432=CARTESIAN_POINT ( 'NONE',  ( -12.18398860626900060, 28.73617430169795739, 5.000000000000000000 ) ) ;
#44433=DIRECTION ( 'NONE',  ( 0.7071067811865487940, 0.7071067811865463515, -0.000000000000000000 ) ) ;
#44434=AXIS2_PLACEMENT_3D ( 'NONE', #63580, #115734, #139707 ) ;
#44435=DIRECTION ( 'NONE',  ( 0.7071067811865486830, -0.7071067811865464625, -0.000000000000000000 ) ) ;
#44436=VECTOR ( 'NONE', #96592, 1000.000000000000000 ) ;
#44437=DIRECTION ( 'NONE',  ( -0.000000000000000000, 0.3543493200069153248, 0.9351131265310292928 ) ) ;
#44439=FACE_OUTER_BOUND ( 'NONE', #63661, .T. ) ;
#44440=ORIENTED_EDGE ( 'NONE', *, *, #46790, .T. ) ;
#44441=EDGE_LOOP ( 'NONE', ( #118807, #48674, #19725, #83975 ) ) ;
#44442=DIRECTION ( 'NONE',  ( -0.000000000000000000, 0.3543493200069153248, 0.9351131265310292928 ) ) ;
#44443=EDGE_LOOP ( 'NONE', ( #35230, #110435, #40396, #125901 ) ) ;
#44445=VERTEX_POINT ( 'NONE', #38666 ) ;
#44447=LINE ( 'NONE', #108922, #27034 ) ;
#44448=CARTESIAN_POINT ( 'NONE',  ( 0.000000000000000000, 0.000000000000000000, 5.000000000000000000 ) ) ;
#44449=EDGE_LOOP ( 'NONE', ( #1621, #19059, #70254, #65073 ) ) ;
#44450=DIRECTION ( 'NONE',  ( 1.000000000000000000, 0.000000000000000000, 0.000000000000000000 ) ) ;
#44452=DIRECTION ( 'NONE',  ( 0.6830127018922181881, 0.6830127018922202975, -0.2588190451025214056 ) ) ;
#44456=LINE ( 'NONE', #111833, #125604 ) ;
#44458=VECTOR ( 'NONE', #13008, 1000.000000000000000 ) ;
#44459=DIRECTION ( 'NONE',  ( 0.7071067811865487940, -0.7071067811865463515, 0.000000000000000000 ) ) ;
#44461=PLANE ( 'NONE',  #101359 ) ;
#44463=DIRECTION ( 'NONE',  ( -0.7071067811865486830, 0.7071067811865464625, 0.000000000000000000 ) ) ;
#44464=LINE ( 'NONE', #132904, #43875 ) ;
#44465=ORIENTED_EDGE ( 'NONE', *, *, #10619, .T. ) ;
#44466=ORIENTED_EDGE ( 'NONE', *, *, #65344, .F. ) ;
#44468=EDGE_CURVE ( 'NONE', #47327, #142384, #114074, .T. ) ;
#44469=DIRECTION ( 'NONE',  ( 0.7071067811865487940, -0.7071067811865463515, 0.000000000000000000 ) ) ;
#44470=ORIENTED_EDGE ( 'NONE', *, *, #59209, .F. ) ;
#44471=AXIS2_PLACEMENT_3D ( 'NONE', #136555, #83652, #138728 ) ;
#44472=VECTOR ( 'NONE', #103020, 1000.000000000000227 ) ;
#44473=DIRECTION ( 'NONE',  ( 0.7071067811865486830, -0.7071067811865464625, -0.000000000000000000 ) ) ;
#44474=FACE_OUTER_BOUND ( 'NONE', #13576, .T. ) ;
#44475=AXIS2_PLACEMENT_3D ( 'NONE', #132959, #56117, #35070 ) ;
#44476=EDGE_CURVE ( 'NONE', #9428, #138835, #36519, .T. ) ;
#44478=ORIENTED_EDGE ( 'NONE', *, *, #57872, .T. ) ;
#44479=EDGE_CURVE ( 'NONE', #100907, #34581, #26364, .T. ) ;
#44480=CARTESIAN_POINT ( 'NONE',  ( 15.21590231913187630, -1.409216073889147491, 4.328383627671532174 ) ) ;
#44481=VERTEX_POINT ( 'NONE', #70621 ) ;
#44483=EDGE_LOOP ( 'NONE', ( #97070, #109743, #88933, #132190 ) ) ;
#44484=VECTOR ( 'NONE', #26599, 1000.000000000000227 ) ;
#44487=DIRECTION ( 'NONE',  ( -0.7071067811865486830, -0.7071067811865464625, 0.000000000000000000 ) ) ;
#44490=EDGE_CURVE ( 'NONE', #62199, #122251, #14762, .T. ) ;
#44491=DIRECTION ( 'NONE',  ( -0.3543493200069162685, -0.000000000000000000, -0.9351131265310288487 ) ) ;
#44492=ORIENTED_EDGE ( 'NONE', *, *, #122229, .T. ) ;
#44494=EDGE_CURVE ( 'NONE', #40635, #45746, #16910, .T. ) ;
#44495=EDGE_CURVE ( 'NONE', #39017, #45797, #105333, .T. ) ;
#44496=VERTEX_POINT ( 'NONE', #61864 ) ;
#44498=CARTESIAN_POINT ( 'NONE',  ( -38.99451991528749062, 28.92564299267965211, 4.000000000000000000 ) ) ;
#44499=CARTESIAN_POINT ( 'NONE',  ( 8.207106781186489286, -14.24070752338414181, 5.000000000000000000 ) ) ;
#44500=CARTESIAN_POINT ( 'NONE',  ( -5.816011393731002066, 28.73617430169783304, 5.000000000000000000 ) ) ;
#44501=CARTESIAN_POINT ( 'NONE',  ( -16.82816939922340893, 12.75929247661558819, 4.000000000000000000 ) ) ;
#44502=EDGE_CURVE ( 'NONE', #59940, #80353, #50264, .T. ) ;
#44503=ADVANCED_FACE ( 'NONE', ( #116928 ), #94453, .F. ) ;
#44504=EDGE_LOOP ( 'NONE', ( #111072, #60424, #58341, #1546 ) ) ;
#44508=EDGE_CURVE ( 'NONE', #42793, #121499, #83622, .T. ) ;
#44509=CARTESIAN_POINT ( 'NONE',  ( -21.18398860626899349, 28.73617430169802134, 5.000000000000000000 ) ) ;
#44510=FACE_OUTER_BOUND ( 'NONE', #66001, .T. ) ;
#44512=ORIENTED_EDGE ( 'NONE', *, *, #16145, .T. ) ;
#44513=DIRECTION ( 'NONE',  ( -0.6830127018922180770, -0.6830127018922204085, -0.2588190451025213501 ) ) ;
#44515=ORIENTED_EDGE ( 'NONE', *, *, #56477, .T. ) ;
#44517=ADVANCED_FACE ( 'NONE', ( #137269 ), #5288, .T. ) ;
#44518=VECTOR ( 'NONE', #111317, 1000.000000000000000 ) ;
#44519=DIRECTION ( 'NONE',  ( -0.000000000000000000, 0.000000000000000000, 1.000000000000000000 ) ) ;
#44520=ORIENTED_EDGE ( 'NONE', *, *, #108266, .F. ) ;
#44521=AXIS2_PLACEMENT_3D ( 'NONE', #76094, #61671, #140617 ) ;
#44522=CARTESIAN_POINT ( 'NONE',  ( -44.99451991528749772, 28.92564299267969474, 4.000000000000000000 ) ) ;
#44523=DIRECTION ( 'NONE',  ( 0.7071067811865486830, -0.7071067811865464625, -0.000000000000000000 ) ) ;
#44524=PLANE ( 'NONE',  #134180 ) ;
#44525=VECTOR ( 'NONE', #111083, 1000.000000000000000 ) ;
#44526=CARTESIAN_POINT ( 'NONE',  ( -60.18398860626900415, 28.73617430169829490, 5.000000000000000000 ) ) ;
#44527=FACE_BOUND ( 'NONE', #56530, .T. ) ;
#44528=CARTESIAN_POINT ( 'NONE',  ( -81.48921356237309510, -27.52281430457112066, 5.000000000000000000 ) ) ;
#44529=DIRECTION ( 'NONE',  ( -0.000000000000000000, 0.3543493200069153248, 0.9351131265310292928 ) ) ;
#44530=CARTESIAN_POINT ( 'NONE',  ( 29.52487387214936376, 14.25929247661557397, 9.797011795316704408 ) ) ;
#44531=CARTESIAN_POINT ( 'NONE',  ( -1.499999999999987566, -7.420205493532900931, -2.617629953481256599 ) ) ;
#44532=EDGE_LOOP ( 'NONE', ( #111454, #42103, #16699, #21340 ) ) ;
#44533=EDGE_CURVE ( 'NONE', #8796, #47010, #50971, .T. ) ;
#44534=AXIS2_PLACEMENT_3D ( 'NONE', #134206, #142242, #12401 ) ;
#44537=ORIENTED_EDGE ( 'NONE', *, *, #100455, .T. ) ;
#44538=ORIENTED_EDGE ( 'NONE', *, *, #21484, .T. ) ;
#44540=VERTEX_POINT ( 'NONE', #49572 ) ;
#44541=CARTESIAN_POINT ( 'NONE',  ( 84.18398860626899705, 28.73617430169846187, 5.000000000000000000 ) ) ;
#44542=CARTESIAN_POINT ( 'NONE',  ( -3.792893218813422340, 9.759292476615620160, 5.000000000000000000 ) ) ;
#44543=VECTOR ( 'NONE', #85274, 1000.000000000000000 ) ;
#44545=EDGE_LOOP ( 'NONE', ( #125795, #51782, #21528, #29535 ) ) ;
#44546=CARTESIAN_POINT ( 'NONE',  ( 17.99999999999986855, -22.06887692260758271, 4.000000000000000000 ) ) ;
#44547=VECTOR ( 'NONE', #55116, 1000.000000000000227 ) ;
#44548=DIRECTION ( 'NONE',  ( -0.000000000000000000, -0.3543493200069152693, 0.9351131265310292928 ) ) ;
#44549=EDGE_CURVE ( 'NONE', #12475, #57697, #92303, .T. ) ;
#44550=CARTESIAN_POINT ( 'NONE',  ( 18.48921356237309510, -27.52281430457068367, 5.000000000000000000 ) ) ;
#44551=DIRECTION ( 'NONE',  ( 0.3543493200069162685, -0.000000000000000000, -0.9351131265310288487 ) ) ;
#44552=DIRECTION ( 'NONE',  ( -0.7071067811865486830, -0.7071067811865464625, -0.000000000000000000 ) ) ;
#44553=FACE_OUTER_BOUND ( 'NONE', #63281, .T. ) ;
#44554=ADVANCED_FACE ( 'NONE', ( #125684 ), #114760, .T. ) ;
#44555=DIRECTION ( 'NONE',  ( 0.6830127018922181881, 0.6830127018922202975, -0.2588190451025214056 ) ) ;
#44556=DIRECTION ( 'NONE',  ( 0.6830127018922180770, -0.6830127018922204085, -0.2588190451025213501 ) ) ;
#44558=VECTOR ( 'NONE', #34770, 1000.000000000000000 ) ;
#44559=DIRECTION ( 'NONE',  ( -0.000000000000000000, 0.000000000000000000, 1.000000000000000000 ) ) ;
#44560=EDGE_LOOP ( 'NONE', ( #9282, #12767, #82876, #38886 ) ) ;
#44561=( BOUNDED_CURVE ( )  B_SPLINE_CURVE ( 3, ( #120919, #78150, #122324, #87584 ),
 .UNSPECIFIED., .F., .T. ) 
 B_SPLINE_CURVE_WITH_KNOTS ( ( 4, 4 ),
 ( 1.864375635226937611, 1.933014472006542750 ),
 .UNSPECIFIED. ) 
 CURVE ( )  GEOMETRIC_REPRESENTATION_ITEM ( )  RATIONAL_B_SPLINE_CURVE ( ( 1.000000000000000000, 0.9996074310407765395, 0.9996074310407765395, 1.000000000000000000 ) ) 
 REPRESENTATION_ITEM ( '' )  );
#44562=CARTESIAN_POINT ( 'NONE',  ( -26.99451991528749417, 28.92564299267956685, 4.000000000000000000 ) ) ;
#44564=ORIENTED_EDGE ( 'NONE', *, *, #1250, .T. ) ;
#44565=ORIENTED_EDGE ( 'NONE', *, *, #75145, .F. ) ;
#44567=AXIS2_PLACEMENT_3D ( 'NONE', #69789, #49465, #37115 ) ;
#44569=CARTESIAN_POINT ( 'NONE',  ( -3.299744871391591339, -27.71228299555208352, 4.000000000000000000 ) ) ;
#44570=EDGE_CURVE ( 'NONE', #44719, #128385, #82201, .T. ) ;
#44571=CARTESIAN_POINT ( 'NONE',  ( 18.70612307739183322, 22.22500000000000142, 4.000000000000000000 ) ) ;
#44573=DIRECTION ( 'NONE',  ( 0.6830127018922180770, -0.6830127018922204085, -0.2588190451025213501 ) ) ;
#44574=VERTEX_POINT ( 'NONE', #137985 ) ;
#44575=EDGE_CURVE ( 'NONE', #80908, #43048, #109617, .T. ) ;
#44576=PLANE ( 'NONE',  #82822 ) ;
#44578=CARTESIAN_POINT ( 'NONE',  ( -8.999999999999936051, 18.08204922493372990, 0.9627537363045106655 ) ) ;
#44579=LINE ( 'NONE', #101041, #70702 ) ;
#44580=VECTOR ( 'NONE', #126745, 1000.000000000000114 ) ;
#44581=VECTOR ( 'NONE', #119932, 1000.000000000000227 ) ;
#44582=LINE ( 'NONE', #130859, #107263 ) ;
#44583=VERTEX_POINT ( 'NONE', #74889 ) ;
#44584=VECTOR ( 'NONE', #74621, 1000.000000000000227 ) ;
#44585=ORIENTED_EDGE ( 'NONE', *, *, #134100, .F. ) ;
#44586=CARTESIAN_POINT ( 'NONE',  ( -32.99999999999977263, 16.93112307739200872, 4.000000000000000000 ) ) ;
#44587=VECTOR ( 'NONE', #59040, 1000.000000000000000 ) ;
#44588=DIRECTION ( 'NONE',  ( -0.7071067811865486830, 0.7071067811865464625, 0.000000000000000000 ) ) ;
#44590=EDGE_LOOP ( 'NONE', ( #141527, #106401, #107079 ) ) ;
#44591=LINE ( 'NONE', #31010, #68758 ) ;
#44592=ORIENTED_EDGE ( 'NONE', *, *, #68731, .F. ) ;
#44593=EDGE_CURVE ( 'NONE', #13610, #24129, #117607, .T. ) ;
#44594=PLANE ( 'NONE',  #109702 ) ;
#44595=CARTESIAN_POINT ( 'NONE',  ( 34.92499999999998295, 2.816654386410421207, 4.500000000000000888 ) ) ;
#44596=DIRECTION ( 'NONE',  ( 0.7071067811865487940, 0.7071067811865463515, -0.000000000000000000 ) ) ;
#44597=VECTOR ( 'NONE', #11786, 1000.000000000000000 ) ;
#44599=LINE ( 'NONE', #33001, #6757 ) ;
#44601=DIRECTION ( 'NONE',  ( 0.6830127018922180770, -0.6830127018922204085, -0.2588190451025213501 ) ) ;
#44602=DIRECTION ( 'NONE',  ( 0.7071067811865486830, -0.7071067811865464625, -0.000000000000000000 ) ) ;
#44603=EDGE_CURVE ( 'NONE', #103813, #115637, #42253, .T. ) ;
#44604=LINE ( 'NONE', #88795, #11266 ) ;
#44605=ORIENTED_EDGE ( 'NONE', *, *, #76279, .F. ) ;
#44606=CARTESIAN_POINT ( 'NONE',  ( -26.99999999999980105, 2.966399257802232459, 5.000000000000000000 ) ) ;
#44607=EDGE_CURVE ( 'NONE', #129536, #25281, #14196, .T. ) ;
#44608=ORIENTED_EDGE ( 'NONE', *, *, #95558, .T. ) ;
#44609=CARTESIAN_POINT ( 'NONE',  ( 24.79289321881328334, -11.24070752338417378, 5.000000000000000000 ) ) ;
#44611=DIRECTION ( 'NONE',  ( 1.000000000000000000, 0.000000000000000000, 0.000000000000000000 ) ) ;
#44612=DIRECTION ( 'NONE',  ( 1.000000000000000000, -0.000000000000000000, -0.000000000000000000 ) ) ;
#44613=EDGE_LOOP ( 'NONE', ( #28478, #93137, #127936, #127992 ) ) ;
#44614=CARTESIAN_POINT ( 'NONE',  ( 36.48921356237310221, -27.52281430457080802, 5.000000000000000000 ) ) ;
#44615=CARTESIAN_POINT ( 'NONE',  ( 9.183988606268997046, 28.73617430169793607, 5.000000000000000000 ) ) ;
#44616=CARTESIAN_POINT ( 'NONE',  ( -72.18398860626899705, 28.73617430169837661, 5.000000000000000000 ) ) ;
#44617=EDGE_LOOP ( 'NONE', ( #10148, #27644, #55268, #24104 ) ) ;
#44618=DIRECTION ( 'NONE',  ( -0.000000000000000000, -0.3543493200069152693, 0.9351131265310292928 ) ) ;
#44619=PLANE ( 'NONE',  #115925 ) ;
#44620=DIRECTION ( 'NONE',  ( -0.7071067811865486830, -0.7071067811865464625, -0.000000000000000000 ) ) ;
#44622=FACE_OUTER_BOUND ( 'NONE', #52050, .T. ) ;
#44624=EDGE_CURVE ( 'NONE', #74278, #137039, #129219, .T. ) ;
#44625=CARTESIAN_POINT ( 'NONE',  ( -0.7201904164744685755, -22.22500000000000142, -7.961480994124567445 ) ) ;
#44626=CARTESIAN_POINT ( 'NONE',  ( -7.828169399223469327, -17.24070752338410628, 4.000000000000000000 ) ) ;
#44627=EDGE_CURVE ( 'NONE', #100863, #70912, #30659, .T. ) ;
#44628=DIRECTION ( 'NONE',  ( 0.7071067811865486830, -0.7071067811865464625, -0.000000000000000000 ) ) ;
#44629=DIRECTION ( 'NONE',  ( 0.6830127018922181881, 0.6830127018922202975, -0.2588190451025214056 ) ) ;
#44630=AXIS2_PLACEMENT_3D ( 'NONE', #67191, #111388, #131739 ) ;
#44633=VERTEX_POINT ( 'NONE', #20452 ) ;
#44634=CARTESIAN_POINT ( 'NONE',  ( 1.499999999999980460, 22.08746187583903975, 4.000000000000000000 ) ) ;
#44635=DIRECTION ( 'NONE',  ( 0.7071067811865487940, 0.7071067811865463515, 0.000000000000000000 ) ) ;
#44637=LINE ( 'NONE', #23544, #29881 ) ;
#44638=CARTESIAN_POINT ( 'NONE',  ( -7.828169399223476432, 3.759292476615681888, 4.000000000000000000 ) ) ;
#44640=ADVANCED_FACE ( 'NONE', ( #140804 ), #62567, .F. ) ;
#44641=CARTESIAN_POINT ( 'NONE',  ( -32.99999999999977263, 17.96639925780207747, 5.000000000000000000 ) ) ;
#44642=CARTESIAN_POINT ( 'NONE',  ( -29.99999999999978684, 11.58746187583912679, 4.000000000000000000 ) ) ;
#44643=ORIENTED_EDGE ( 'NONE', *, *, #138941, .F. ) ;
#44644=EDGE_LOOP ( 'NONE', ( #51526, #97017, #61574, #4161 ) ) ;
#44645=PLANE ( 'NONE',  #99619 ) ;
#44646=PLANE ( 'NONE',  #106939 ) ;
#44648=DIRECTION ( 'NONE',  ( -0.6830127018922180770, -0.6830127018922204085, -0.2588190451025213501 ) ) ;
#44651=DIRECTION ( 'NONE',  ( 0.7071067811865487940, -0.7071067811865463515, 0.000000000000000000 ) ) ;
#44652=CARTESIAN_POINT ( 'NONE',  ( -25.49999999999982236, 18.43112307739199451, 4.000000000000000000 ) ) ;
#44653=VERTEX_POINT ( 'NONE', #52380 ) ;
#44655=LINE ( 'NONE', #32316, #137234 ) ;
#44656=LINE ( 'NONE', #14098, #32404 ) ;
#44657=LINE ( 'NONE', #77964, #61403 ) ;
#44658=AXIS2_PLACEMENT_3D ( 'NONE', #55536, #11267, #401 ) ;
#44659=EDGE_LOOP ( 'NONE', ( #81083, #3162, #96886, #108466 ) ) ;
#44660=CARTESIAN_POINT ( 'NONE',  ( 29.67183060077626422, -0.7407075233842770334, 4.000000000000000000 ) ) ;
#44661=EDGE_LOOP ( 'NONE', ( #124137, #12842, #14218 ) ) ;
#44662=EDGE_CURVE ( 'NONE', #110589, #24532, #139441, .T. ) ;
#44665=PLANE ( 'NONE',  #91709 ) ;
#44666=EDGE_LOOP ( 'NONE', ( #18212, #109786, #128975, #44122 ) ) ;
#44667=VECTOR ( 'NONE', #114360, 1000.000000000000000 ) ;
#44668=CARTESIAN_POINT ( 'NONE',  ( 18.18398860626898994, 28.73617430169800002, 5.000000000000000000 ) ) ;
#44669=FACE_OUTER_BOUND ( 'NONE', #107023, .T. ) ;
#44671=LINE ( 'NONE', #30912, #111094 ) ;
#44672=CARTESIAN_POINT ( 'NONE',  ( -63.48921356237309510, -27.52281430457099631, 5.000000000000000000 ) ) ;
#44673=ADVANCED_FACE ( 'NONE', ( #63308 ), #118342, .T. ) ;
#44674=CARTESIAN_POINT ( 'NONE',  ( 34.42499999999998295, -9.022814304570511368, 5.000000000000000000 ) ) ;
#44675=ORIENTED_EDGE ( 'NONE', *, *, #126154, .F. ) ;
#44677=CARTESIAN_POINT ( 'NONE',  ( 8.999999999999937828, -15.41253812416059787, 4.000000000000000000 ) ) ;
#44678=VECTOR ( 'NONE', #103097, 1000.000000000000000 ) ;
#44679=DIRECTION ( 'NONE',  ( 0.7071067811865487940, 0.7071067811865463515, 0.000000000000000000 ) ) ;
#44680=CARTESIAN_POINT ( 'NONE',  ( -35.99451991528749772, 28.92564299267963079, 4.000000000000000000 ) ) ;
#44681=ORIENTED_EDGE ( 'NONE', *, *, #60372, .F. ) ;
#44683=ORIENTED_EDGE ( 'NONE', *, *, #64980, .T. ) ;
#44684=EDGE_CURVE ( 'NONE', #66820, #49172, #96566, .T. ) ;
#44686=VERTEX_POINT ( 'NONE', #98044 ) ;
#44690=EDGE_CURVE ( 'NONE', #46869, #140963, #131386, .T. ) ;
#44691=PLANE ( 'NONE',  #105929 ) ;
#44693=ORIENTED_EDGE ( 'NONE', *, *, #142369, .F. ) ;
#44694=ORIENTED_EDGE ( 'NONE', *, *, #32951, .T. ) ;
#44697=CARTESIAN_POINT ( 'NONE',  ( -7.499999999999945821, -20.53675388469231322, 2.352720554255875562 ) ) ;
#44698=AXIS2_PLACEMENT_3D ( 'NONE', #60447, #136527, #124240 ) ;
#44699=VECTOR ( 'NONE', #63279, 1000.000000000000000 ) ;
#44701=ORIENTED_EDGE ( 'NONE', *, *, #131723, .F. ) ;
#44702=DIRECTION ( 'NONE',  ( 0.7071067811865487940, 0.7071067811865463515, 0.000000000000000000 ) ) ;
#44704=DIRECTION ( 'NONE',  ( 0.7071067811865487940, 0.7071067811865463515, 0.000000000000000000 ) ) ;
#44705=DIRECTION ( 'NONE',  ( 0.7071067811865487940, 0.7071067811865463515, 0.000000000000000000 ) ) ;
#44706=AXIS2_PLACEMENT_3D ( 'NONE', #111463, #1942, #78867 ) ;
#44708=ORIENTED_EDGE ( 'NONE', *, *, #53464, .T. ) ;
#44709=EDGE_CURVE ( 'NONE', #44574, #139771, #122631, .T. ) ;
#44710=EDGE_CURVE ( 'NONE', #38177, #45110, #89998, .T. ) ;
#44711=FACE_BOUND ( 'NONE', #124200, .T. ) ;
#44713=CARTESIAN_POINT ( 'NONE',  ( -31.49999999999979039, -7.420205493532932017, -2.617629953481324101 ) ) ;
#44714=CARTESIAN_POINT ( 'NONE',  ( -17.21574841994372562, 22.22500000000000142, 11.71069743027089061 ) ) ;
#44715=CARTESIAN_POINT ( 'NONE',  ( -7.171830600776418763, 21.75929247661548871, 4.000000000000000000 ) ) ;
#44716=ADVANCED_FACE ( 'NONE', ( #134246 ), #55255, .F. ) ;
#44717=CARTESIAN_POINT ( 'NONE',  ( 20.99999999999985079, -21.03360074219752462, 5.000000000000000000 ) ) ;
#44719=VERTEX_POINT ( 'NONE', #21894 ) ;
#44720=ORIENTED_EDGE ( 'NONE', *, *, #143162, .T. ) ;
#44722=VERTEX_POINT ( 'NONE', #12440 ) ;
#44723=DIRECTION ( 'NONE',  ( -0.000000000000000000, 0.000000000000000000, 1.000000000000000000 ) ) ;
#44724=ORIENTED_EDGE ( 'NONE', *, *, #127366, .F. ) ;
#44725=PLANE ( 'NONE',  #141900 ) ;
#44728=DIRECTION ( 'NONE',  ( -0.7071067811865486830, 0.7071067811865464625, 0.000000000000000000 ) ) ;
#44729=EDGE_LOOP ( 'NONE', ( #48603, #83775, #62174, #128259 ) ) ;
#44730=CARTESIAN_POINT ( 'NONE',  ( 0.7061230773919568993, 22.22500000000000142, 4.000000000000000000 ) ) ;
#44731=CARTESIAN_POINT ( 'NONE',  ( 15.00548008471250228, 28.92564299267927552, 4.000000000000000000 ) ) ;
#44732=LINE ( 'NONE', #127585, #12960 ) ;
#44733=DIRECTION ( 'NONE',  ( -0.7071067811865486830, 0.7071067811865464625, 0.000000000000000000 ) ) ;
#44734=CARTESIAN_POINT ( 'NONE',  ( -15.79333936457836707, 21.75929247661549937, 4.998822639870700080 ) ) ;
#44735=CARTESIAN_POINT ( 'NONE',  ( -20.77868544475317947, 8.889383937919465239, 4.212719859983343973 ) ) ;
#44736=EDGE_CURVE ( 'NONE', #138729, #136079, #77029, .T. ) ;
#44737=CARTESIAN_POINT ( 'NONE',  ( 2.510786437626908008, -27.52281430457053446, 5.000000000000000000 ) ) ;
#44738=DIRECTION ( 'NONE',  ( -0.000000000000000000, 0.000000000000000000, 1.000000000000000000 ) ) ;
#44739=VERTEX_POINT ( 'NONE', #66843 ) ;
#44740=FACE_OUTER_BOUND ( 'NONE', #123726, .T. ) ;
#44741=CARTESIAN_POINT ( 'NONE',  ( 26.29289321881327623, -3.740707523384243505, 5.000000000000000000 ) ) ;
#44742=VERTEX_POINT ( 'NONE', #99436 ) ;
#44743=ORIENTED_EDGE ( 'NONE', *, *, #5050, .F. ) ;
#44744=ORIENTED_EDGE ( 'NONE', *, *, #44245, .T. ) ;
#44746=VERTEX_POINT ( 'NONE', #87873 ) ;
#44747=ADVANCED_FACE ( 'NONE', ( #24752 ), #110310, .F. ) ;
#44749=DIRECTION ( 'NONE',  ( 0.7071067811865486830, -0.7071067811865464625, -0.000000000000000000 ) ) ;
#44752=CARTESIAN_POINT ( 'NONE',  ( 36.29974487139159578, -27.71228299555231445, 4.000000000000000000 ) ) ;
#44754=ADVANCED_FACE ( 'NONE', ( #34939 ), #56723, .F. ) ;
#44755=VECTOR ( 'NONE', #74993, 1000.000000000000000 ) ;
#44756=EDGE_LOOP ( 'NONE', ( #109580, #107068, #123158, #80882 ) ) ;
#44757=DIRECTION ( 'NONE',  ( 0.7071067811865487940, -0.7071067811865463515, 0.000000000000000000 ) ) ;
#44759=CARTESIAN_POINT ( 'NONE',  ( 25.00934544866806064, 2.809161053235903704, 4.346514962826528716 ) ) ;
#44760=EDGE_LOOP ( 'NONE', ( #22725, #15060, #105210, #71362 ) ) ;
#44762=LINE ( 'NONE', #100530, #77632 ) ;
#44763=ORIENTED_EDGE ( 'NONE', *, *, #137972, .T. ) ;
#44764=CARTESIAN_POINT ( 'NONE',  ( 23.50183651486029746, -17.24070752338409918, 8.407044977365172755 ) ) ;
#44766=EDGE_LOOP ( 'NONE', ( #79828, #24021, #55624, #114857 ) ) ;
#44767=ORIENTED_EDGE ( 'NONE', *, *, #110314, .T. ) ;
#44768=ORIENTED_EDGE ( 'NONE', *, *, #88062, .T. ) ;
#44771=FACE_OUTER_BOUND ( 'NONE', #48447, .T. ) ;
#44772=ADVANCED_FACE ( 'NONE', ( #77727 ), #121902, .F. ) ;
#44773=CARTESIAN_POINT ( 'NONE',  ( 34.92499999999997584, 13.80009451602703408, 4.759050581649328038 ) ) ;
#44775=DIRECTION ( 'NONE',  ( 1.000000000000000000, 0.000000000000000000, 0.000000000000000000 ) ) ;
#44776=AXIS2_PLACEMENT_3D ( 'NONE', #38382, #82597, #121625 ) ;
#44777=ORIENTED_EDGE ( 'NONE', *, *, #45723, .F. ) ;
#44779=EDGE_CURVE ( 'NONE', #43782, #94364, #45821, .T. ) ;
#44782=CARTESIAN_POINT ( 'NONE',  ( -2.292893218813438772, 5.259292476615662792, 5.000000000000000000 ) ) ;
#44784=ORIENTED_EDGE ( 'NONE', *, *, #4316, .T. ) ;
#44785=ORIENTED_EDGE ( 'NONE', *, *, #6469, .F. ) ;
#44786=DIRECTION ( 'NONE',  ( 0.7071067811865486830, -0.7071067811865464625, -0.000000000000000000 ) ) ;
#44787=CARTESIAN_POINT ( 'NONE',  ( -9.489213562373095101, -27.52281430457062328, 5.000000000000000000 ) ) ;
#44789=VECTOR ( 'NONE', #49234, 1000.000000000000000 ) ;
#44791=LINE ( 'NONE', #133205, #66823 ) ;
#44792=ADVANCED_FACE ( 'NONE', ( #13139 ), #24050, .F. ) ;
#44794=EDGE_CURVE ( 'NONE', #98171, #102362, #113904, .T. ) ;
#44795=CARTESIAN_POINT ( 'NONE',  ( 33.29974487139158867, -27.71228299555229313, 4.000000000000000000 ) ) ;
#44796=EDGE_CURVE ( 'NONE', #20040, #114456, #2992, .T. ) ;
#44797=CARTESIAN_POINT ( 'NONE',  ( 34.45011844616453800, 16.51628081163733697, 5.000000000000001776 ) ) ;
#44798=CARTESIAN_POINT ( 'NONE',  ( 24.48921356237309510, -27.52281430457072631, 5.000000000000000000 ) ) ;
#44799=FACE_OUTER_BOUND ( 'NONE', #106982, .T. ) ;
#44800=ORIENTED_EDGE ( 'NONE', *, *, #53652, .F. ) ;
#44801=CARTESIAN_POINT ( 'NONE',  ( -34.42500000000001137, -22.22500000000000142, 5.000000000000000000 ) ) ;
#44802=VECTOR ( 'NONE', #31610, 1000.000000000000000 ) ;
#44804=VERTEX_POINT ( 'NONE', #26894 ) ;
#44805=CARTESIAN_POINT ( 'NONE',  ( 27.98155265364313848, 18.75929247661553134, 20.33588619593436775 ) ) ;
#44806=ORIENTED_EDGE ( 'NONE', *, *, #109008, .F. ) ;
#44808=CARTESIAN_POINT ( 'NONE',  ( 57.29974487139158157, -27.71228299555246011, 4.000000000000000000 ) ) ;
#44810=ORIENTED_EDGE ( 'NONE', *, *, #19150, .T. ) ;
#44811=ADVANCED_FACE ( 'NONE', ( #82718 ), #104442, .F. ) ;
#44812=CARTESIAN_POINT ( 'NONE',  ( 0.000000000000000000, 0.000000000000000000, 5.000000000000000000 ) ) ;
#44813=DIRECTION ( 'NONE',  ( -0.6830127018922180770, -0.6830127018922204085, -0.2588190451025213501 ) ) ;
#44814=ORIENTED_EDGE ( 'NONE', *, *, #26658, .T. ) ;
#44815=CARTESIAN_POINT ( 'NONE',  ( 8.510786437626906675, -27.52281430457049183, 5.000000000000000000 ) ) ;
#44816=ORIENTED_EDGE ( 'NONE', *, *, #2410, .F. ) ;
#44817=CARTESIAN_POINT ( 'NONE',  ( 3.489213562373097322, -27.52281430457057709, 5.000000000000000000 ) ) ;
#44819=ORIENTED_EDGE ( 'NONE', *, *, #70723, .T. ) ;
#44820=DIRECTION ( 'NONE',  ( -0.000000000000000000, 0.000000000000000000, 1.000000000000000000 ) ) ;
#44822=AXIS2_PLACEMENT_3D ( 'NONE', #105196, #114634, #49432 ) ;
#44823=CARTESIAN_POINT ( 'NONE',  ( -14.70025512860841133, -27.71228299555195917, 4.000000000000000000 ) ) ;
#44825=DIRECTION ( 'NONE',  ( -0.7071067811865487940, 0.7071067811865463515, -0.000000000000000000 ) ) ;
#44826=FACE_OUTER_BOUND ( 'NONE', #123817, .T. ) ;
#44829=CARTESIAN_POINT ( 'NONE',  ( 24.79289321881328334, 12.75929247661559529, 5.000000000000000000 ) ) ;
#44830=CARTESIAN_POINT ( 'NONE',  ( 39.48921356237310221, -27.52281430457082934, 5.000000000000000000 ) ) ;
#44832=VECTOR ( 'NONE', #38127, 1000.000000000000227 ) ;
#44834=CARTESIAN_POINT ( 'NONE',  ( 8.999999999999937828, -22.06887692260758982, 4.000000000000000000 ) ) ;
#44835=ORIENTED_EDGE ( 'NONE', *, *, #39907, .T. ) ;
#44836=VECTOR ( 'NONE', #136528, 1000.000000000000000 ) ;
#44838=DIRECTION ( 'NONE',  ( 0.7071067811865486830, -0.7071067811865464625, -0.000000000000000000 ) ) ;
#44839=CARTESIAN_POINT ( 'NONE',  ( 3.005480084712505828, 28.92564299267936079, 4.000000000000000000 ) ) ;
#44840=FACE_OUTER_BOUND ( 'NONE', #69119, .T. ) ;
#44842=ORIENTED_EDGE ( 'NONE', *, *, #25417, .T. ) ;
#44843=DIRECTION ( 'NONE',  ( -0.7071067811865486830, -0.7071067811865464625, 0.000000000000000000 ) ) ;
#44845=VECTOR ( 'NONE', #27232, 1000.000000000000000 ) ;
#44846=EDGE_CURVE ( 'NONE', #99762, #7658, #69722, .T. ) ;
#44847=DIRECTION ( 'NONE',  ( -0.7071067811865486830, -0.7071067811865464625, -0.000000000000000000 ) ) ;
#44849=DIRECTION ( 'NONE',  ( 0.3543493200069162685, -0.000000000000000000, -0.9351131265310288487 ) ) ;
#44850=ORIENTED_EDGE ( 'NONE', *, *, #125258, .T. ) ;
#44853=LINE ( 'NONE', #86171, #72514 ) ;
#44854=DIRECTION ( 'NONE',  ( -0.7071067811865486830, -0.7071067811865464625, 0.000000000000000000 ) ) ;
#44855=CARTESIAN_POINT ( 'NONE',  ( 12.32816939922344446, 17.25929247661554200, 4.000000000000000000 ) ) ;
#44856=VECTOR ( 'NONE', #135964, 999.9999999999998863 ) ;
#44858=EDGE_LOOP ( 'NONE', ( #142668, #90678, #135366, #93276 ) ) ;
#44859=ORIENTED_EDGE ( 'NONE', *, *, #62855, .F. ) ;
#44860=ADVANCED_FACE ( 'NONE', ( #58875 ), #49404, .F. ) ;
#44862=VECTOR ( 'NONE', #81671, 1000.000000000000000 ) ;
#44863=ORIENTED_EDGE ( 'NONE', *, *, #56488, .F. ) ;
#44865=LINE ( 'NONE', #68044, #25431 ) ;
#44866=CARTESIAN_POINT ( 'NONE',  ( -19.49999999999986500, 16.77039438581777375, 0.4657186855308182438 ) ) ;
#44867=EDGE_CURVE ( 'NONE', #14544, #65084, #81302, .T. ) ;
#44868=VECTOR ( 'NONE', #100615, 1000.000000000000000 ) ;
#44870=DIRECTION ( 'NONE',  ( -0.000000000000000000, 0.000000000000000000, 1.000000000000000000 ) ) ;
#44871=VERTEX_POINT ( 'NONE', #26195 ) ;
#44875=( BOUNDED_CURVE ( )  B_SPLINE_CURVE ( 3, ( #115085, #85332, #7027, #96202 ),
 .UNSPECIFIED., .F., .F. ) 
 B_SPLINE_CURVE_WITH_KNOTS ( ( 4, 4 ),
 ( 4.735358278776982566, 4.752060726170250327 ),
 .UNSPECIFIED. ) 
 CURVE ( )  GEOMETRIC_REPRESENTATION_ITEM ( )  RATIONAL_B_SPLINE_CURVE ( ( 1.000000000000000000, 0.9999767524893692361, 0.9999767524893692361, 1.000000000000000000 ) ) 
 REPRESENTATION_ITEM ( '' )  );
#44878=DIRECTION ( 'NONE',  ( -0.7071067811865487940, 0.7071067811865463515, -0.000000000000000000 ) ) ;
#44879=VECTOR ( 'NONE', #48128, 1000.000000000000000 ) ;
#44880=CARTESIAN_POINT ( 'NONE',  ( -30.18398860626900060, 28.73617430169808173, 5.000000000000000000 ) ) ;
#44882=ORIENTED_EDGE ( 'NONE', *, *, #121511, .F. ) ;
#44884=ORIENTED_EDGE ( 'NONE', *, *, #2526, .F. ) ;
#44885=CYLINDRICAL_SURFACE ( 'NONE', #79359, 0.5000000000000004441 ) ;
#44890=DIRECTION ( 'NONE',  ( 0.7071067811865486830, -0.7071067811865464625, -0.000000000000000000 ) ) ;
#44892=EDGE_CURVE ( 'NONE', #76456, #119529, #89757, .T. ) ;
#44893=LINE ( 'NONE', #79665, #107600 ) ;
#44894=VECTOR ( 'NONE', #133853, 1000.000000000000000 ) ;
#44895=ORIENTED_EDGE ( 'NONE', *, *, #76097, .T. ) ;
#44896=ORIENTED_EDGE ( 'NONE', *, *, #21840, .T. ) ;
#44897=DIRECTION ( 'NONE',  ( -0.000000000000000000, -0.3543493200069152693, 0.9351131265310292928 ) ) ;
#44898=ORIENTED_EDGE ( 'NONE', *, *, #140939, .F. ) ;
#44899=ORIENTED_EDGE ( 'NONE', *, *, #136303, .T. ) ;
#44901=VECTOR ( 'NONE', #89086, 1000.000000000000000 ) ;
#44902=DIRECTION ( 'NONE',  ( 1.000000000000000000, 0.000000000000000000, 0.000000000000000000 ) ) ;
#44904=LINE ( 'NONE', #112950, #110754 ) ;
#44905=DIRECTION ( 'NONE',  ( -0.7071067811865486830, -0.7071067811865464625, 0.000000000000000000 ) ) ;
#44907=ADVANCED_FACE ( 'NONE', ( #100657 ), #35428, .F. ) ;
#44910=ORIENTED_EDGE ( 'NONE', *, *, #22341, .F. ) ;
#44911=VERTEX_POINT ( 'NONE', #102076 ) ;
#44912=LINE ( 'NONE', #35450, #126714 ) ;
#44913=ORIENTED_EDGE ( 'NONE', *, *, #50250, .T. ) ;
#44914=DIRECTION ( 'NONE',  ( 1.000000000000000000, 0.000000000000000000, 0.000000000000000000 ) ) ;
#44917=LINE ( 'NONE', #89098, #103736 ) ;
#44919=ORIENTED_EDGE ( 'NONE', *, *, #73436, .F. ) ;
#44920=VECTOR ( 'NONE', #49160, 1000.000000000000227 ) ;
#44921=ORIENTED_EDGE ( 'NONE', *, *, #138664, .T. ) ;
#44922=CARTESIAN_POINT ( 'NONE',  ( -9.183988606268997046, 28.73617430169793607, 5.000000000000000000 ) ) ;
#44923=VECTOR ( 'NONE', #60122, 1000.000000000000000 ) ;
#44924=DIRECTION ( 'NONE',  ( -0.7071067811865487940, 0.7071067811865463515, 0.000000000000000000 ) ) ;
#44925=FACE_OUTER_BOUND ( 'NONE', #34064, .T. ) ;
#44926=LINE ( 'NONE', #132634, #24255 ) ;
#44927=EDGE_CURVE ( 'NONE', #28039, #46695, #99932, .T. ) ;
#44932=DIRECTION ( 'NONE',  ( 0.7071067811865487940, 0.7071067811865463515, 0.000000000000000000 ) ) ;
#44933=ORIENTED_EDGE ( 'NONE', *, *, #34944, .T. ) ;
#44934=LINE ( 'NONE', #45625, #105901 ) ;
#44935=VECTOR ( 'NONE', #132114, 1000.000000000000000 ) ;
#44936=LINE ( 'NONE', #89118, #86573 ) ;
#44937=ADVANCED_FACE ( 'NONE', ( #36121 ), #12899, .F. ) ;
#44938=ORIENTED_EDGE ( 'NONE', *, *, #29487, .T. ) ;
#44939=ORIENTED_EDGE ( 'NONE', *, *, #112637, .F. ) ;
#44940=ORIENTED_EDGE ( 'NONE', *, *, #108598, .T. ) ;
#44941=LINE ( 'NONE', #143470, #26394 ) ;
#44945=LINE ( 'NONE', #55066, #2760 ) ;
#44947=AXIS2_PLACEMENT_3D ( 'NONE', #21179, #29196, #74883 ) ;
#44949=CARTESIAN_POINT ( 'NONE',  ( 0.000000000000000000, 0.000000000000000000, 5.000000000000000000 ) ) ;
#44950=DIRECTION ( 'NONE',  ( 0.6830127018922181881, 0.6830127018922202975, -0.2588190451025214056 ) ) ;
#44952=DIRECTION ( 'NONE',  ( 0.6830127018922181881, 0.6830127018922202975, -0.2588190451025214056 ) ) ;
#44953=ORIENTED_EDGE ( 'NONE', *, *, #24004, .T. ) ;
#44954=LINE ( 'NONE', #24565, #130243 ) ;
#44955=VECTOR ( 'NONE', #111159, 1000.000000000000000 ) ;
#44956=VECTOR ( 'NONE', #81102, 1000.000000000000000 ) ;
#44958=EDGE_LOOP ( 'NONE', ( #106723, #112483, #119406, #96657 ) ) ;
#44961=CARTESIAN_POINT ( 'NONE',  ( -47.99451991528749062, 28.92564299267971251, 4.000000000000000000 ) ) ;
#44962=ORIENTED_EDGE ( 'NONE', *, *, #46178, .F. ) ;
#44963=ORIENTED_EDGE ( 'NONE', *, *, #64287, .F. ) ;
#44968=FACE_OUTER_BOUND ( 'NONE', #89315, .T. ) ;
#44969=DIRECTION ( 'NONE',  ( 0.7071067811865487940, 0.7071067811865463515, 0.000000000000000000 ) ) ;
#44970=ORIENTED_EDGE ( 'NONE', *, *, #33220, .T. ) ;
#44972=EDGE_CURVE ( 'NONE', #101635, #46980, #68069, .T. ) ;
#44973=CARTESIAN_POINT ( 'NONE',  ( 69.29974487139159578, -27.71228299555254537, 4.000000000000000000 ) ) ;
#44974=CARTESIAN_POINT ( 'NONE',  ( 1.499999999999994449, 6.052185695429108669, 5.000000000000000000 ) ) ;
#44975=ORIENTED_EDGE ( 'NONE', *, *, #60587, .F. ) ;
#44977=AXIS2_PLACEMENT_3D ( 'NONE', #116932, #28521, #17601 ) ;
#44978=LINE ( 'NONE', #22425, #141938 ) ;
#44979=ORIENTED_EDGE ( 'NONE', *, *, #73352, .T. ) ;
#44981=CARTESIAN_POINT ( 'NONE',  ( -19.05000000000000071, 3.174999999999997158, 4.000000000000000000 ) ) ;
#44982=EDGE_LOOP ( 'NONE', ( #6926, #43602, #71208, #8886 ) ) ;
#44983=ORIENTED_EDGE ( 'NONE', *, *, #36217, .T. ) ;
#44984=EDGE_CURVE ( 'NONE', #34599, #130423, #44893, .T. ) ;
#44986=CARTESIAN_POINT ( 'NONE',  ( -34.00193056682073944, -22.22500000000000142, 4.500000000000000888 ) ) ;
#44987=VERTEX_POINT ( 'NONE', #80346 ) ;
#44988=CARTESIAN_POINT ( 'NONE',  ( -0.7228143045705931469, -21.72500000000000142, 5.000000000000000000 ) ) ;
#44990=LINE ( 'NONE', #78289, #130900 ) ;
#44991=CARTESIAN_POINT ( 'NONE',  ( -14.70025512860841133, -27.71228299555195917, 4.000000000000000000 ) ) ;
#44992=AXIS2_PLACEMENT_3D ( 'NONE', #275, #133000, #112640 ) ;
#44993=FACE_OUTER_BOUND ( 'NONE', #33372, .T. ) ;
#44994=PLANE ( 'NONE',  #74418 ) ;
#44995=DIRECTION ( 'NONE',  ( 0.7071067811865487940, 0.7071067811865463515, 0.000000000000000000 ) ) ;
#44996=CARTESIAN_POINT ( 'NONE',  ( 33.18398860626899705, 28.73617430169810305, 5.000000000000000000 ) ) ;
#44997=CARTESIAN_POINT ( 'NONE',  ( 57.48921356237308800, -27.52281430457095368, 5.000000000000000000 ) ) ;
#44999=DIRECTION ( 'NONE',  ( -0.000000000000000000, 0.3543493200069153248, 0.9351131265310292928 ) ) ;
#45000=DIRECTION ( 'NONE',  ( 0.7071067811865487940, 0.7071067811865463515, -0.000000000000000000 ) ) ;
#45002=ORIENTED_EDGE ( 'NONE', *, *, #31238, .T. ) ;
#45003=ADVANCED_FACE ( 'NONE', ( #24500 ), #133991, .F. ) ;
#45005=EDGE_LOOP ( 'NONE', ( #136173, #83300, #108995, #91716 ) ) ;
#45007=ORIENTED_EDGE ( 'NONE', *, *, #8124, .T. ) ;
#45008=ORIENTED_EDGE ( 'NONE', *, *, #41640, .F. ) ;
#45009=ORIENTED_EDGE ( 'NONE', *, *, #49665, .T. ) ;
#45010=DIRECTION ( 'NONE',  ( -0.000000000000000000, -0.3543493200069152693, 0.9351131265310292928 ) ) ;
#45011=CARTESIAN_POINT ( 'NONE',  ( -14.68370490163491482, -22.22500000000000142, -2.670183372115248588 ) ) ;
#45012=ORIENTED_EDGE ( 'NONE', *, *, #131479, .T. ) ;
#45013=DIRECTION ( 'NONE',  ( 0.6830127018922180770, -0.6830127018922204085, -0.2588190451025213501 ) ) ;
#45015=CARTESIAN_POINT ( 'NONE',  ( -24.70710678118636494, -15.74070752338412049, 5.000000000000000000 ) ) ;
#45016=PLANE ( 'NONE',  #76742 ) ;
#45017=ORIENTED_EDGE ( 'NONE', *, *, #104661, .F. ) ;
#45018=CARTESIAN_POINT ( 'NONE',  ( 18.18398860626898994, 28.73617430169800002, 5.000000000000000000 ) ) ;
#45020=AXIS2_PLACEMENT_3D ( 'NONE', #59856, #49713, #81627 ) ;
#45021=CARTESIAN_POINT ( 'NONE',  ( -31.17183060077624646, -2.240707523384260824, 4.000000000000000000 ) ) ;
#45023=CARTESIAN_POINT ( 'NONE',  ( 75.18398860626899705, 28.73617430169839793, 5.000000000000000000 ) ) ;
#45024=DIRECTION ( 'NONE',  ( 0.6830127018922180770, -0.6830127018922204085, -0.2588190451025213501 ) ) ;
#45025=CARTESIAN_POINT ( 'NONE',  ( 0.000000000000000000, 0.000000000000000000, 5.000000000000000000 ) ) ;
#45027=ORIENTED_EDGE ( 'NONE', *, *, #136802, .T. ) ;
#45029=EDGE_CURVE ( 'NONE', #89614, #2635, #595, .T. ) ;
#45031=ORIENTED_EDGE ( 'NONE', *, *, #9256, .T. ) ;
#45032=EDGE_CURVE ( 'NONE', #125583, #66944, #102801, .T. ) ;
#45033=VECTOR ( 'NONE', #104850, 1000.000000000000000 ) ;
#45035=CARTESIAN_POINT ( 'NONE',  ( -56.99451991528749062, 28.92564299267978001, 4.000000000000000000 ) ) ;
#45036=ADVANCED_FACE ( 'NONE', ( #132597 ), #133294, .F. ) ;
#45037=EDGE_CURVE ( 'NONE', #119359, #138000, #56478, .T. ) ;
#45038=CARTESIAN_POINT ( 'NONE',  ( 51.18398860626899705, 28.73617430169823095, 5.000000000000000000 ) ) ;
#45040=VECTOR ( 'NONE', #52055, 1000.000000000000000 ) ;
#45041=VERTEX_POINT ( 'NONE', #123132 ) ;
#45042=ORIENTED_EDGE ( 'NONE', *, *, #135533, .T. ) ;
#45043=LINE ( 'NONE', #122538, #76280 ) ;
#45044=FACE_OUTER_BOUND ( 'NONE', #72603, .T. ) ;
#45045=VERTEX_POINT ( 'NONE', #23802 ) ;
#45046=VERTEX_POINT ( 'NONE', #27217 ) ;
#45048=EDGE_CURVE ( 'NONE', #135923, #65251, #51141, .T. ) ;
#45049=VECTOR ( 'NONE', #129050, 999.9999999999998863 ) ;
#45050=EDGE_LOOP ( 'NONE', ( #117875, #41207, #41244, #66066 ) ) ;
#45051=DIRECTION ( 'NONE',  ( -0.7071067811865486830, 0.7071067811865463515, 0.000000000000000000 ) ) ;
#45053=CARTESIAN_POINT ( 'NONE',  ( 45.18398860626900415, 28.73617430169818832, 5.000000000000000000 ) ) ;
#45054=DIRECTION ( 'NONE',  ( -0.7071067811865487940, 0.7071067811865463515, -0.000000000000000000 ) ) ;
#45055=CIRCLE ( 'NONE', #142297, 0.5000000000000000000 ) ;
#45057=AXIS2_PLACEMENT_3D ( 'NONE', #20625, #49906, #88046 ) ;
#45058=VECTOR ( 'NONE', #10825, 999.9999999999998863 ) ;
#45060=ORIENTED_EDGE ( 'NONE', *, *, #26247, .F. ) ;
#45061=CARTESIAN_POINT ( 'NONE',  ( -57.48921356237308800, -27.52281430457095368, 5.000000000000000000 ) ) ;
#45063=ORIENTED_EDGE ( 'NONE', *, *, #141195, .T. ) ;
#45064=EDGE_CURVE ( 'NONE', #31209, #8801, #128000, .T. ) ;
#45065=ORIENTED_EDGE ( 'NONE', *, *, #79162, .T. ) ;
#45066=CARTESIAN_POINT ( 'NONE',  ( 20.99999999999985789, -12.41253812416062807, 4.000000000000000000 ) ) ;
#45067=ORIENTED_EDGE ( 'NONE', *, *, #72997, .F. ) ;
#45068=CARTESIAN_POINT ( 'NONE',  ( 0.000000000000000000, 0.000000000000000000, 5.000000000000000000 ) ) ;
#45069=CARTESIAN_POINT ( 'NONE',  ( -9.758600742197899081, 21.72500000000000853, 5.000000000000000000 ) ) ;
#45070=ADVANCED_FACE ( 'NONE', ( #106185 ), #83790, .F. ) ;
#45071=CARTESIAN_POINT ( 'NONE',  ( -26.99999999999980815, 4.931123077392133069, 4.000000000000000000 ) ) ;
#45072=FACE_BOUND ( 'NONE', #1492, .T. ) ;
#45073=ORIENTED_EDGE ( 'NONE', *, *, #21725, .F. ) ;
#45075=CARTESIAN_POINT ( 'NONE',  ( 2.999999999999992450, 17.96639925780208102, 5.000000000000000000 ) ) ;
#45076=DIRECTION ( 'NONE',  ( -0.3543493200069162685, -0.000000000000000000, -0.9351131265310288487 ) ) ;
#45077=CARTESIAN_POINT ( 'NONE',  ( -15.18398860626900237, 28.73617430169797871, 5.000000000000000000 ) ) ;
#45078=EDGE_LOOP ( 'NONE', ( #56597, #52914, #38067, #117099 ) ) ;
#45079=EDGE_CURVE ( 'NONE', #142885, #141807, #6863, .T. ) ;
#45080=CARTESIAN_POINT ( 'NONE',  ( -31.49999999999977973, -8.947814304570734123, 5.000000000000000000 ) ) ;
#45082=EDGE_CURVE ( 'NONE', #113229, #95696, #94611, .T. ) ;
#45083=ORIENTED_EDGE ( 'NONE', *, *, #82314, .F. ) ;
#45084=VERTEX_POINT ( 'NONE', #40285 ) ;
#45087=ORIENTED_EDGE ( 'NONE', *, *, #31343, .T. ) ;
#45088=CARTESIAN_POINT ( 'NONE',  ( -27.48921356237309155, -27.52281430457074762, 5.000000000000000000 ) ) ;
#45089=PLANE ( 'NONE',  #35782 ) ;
#45090=FACE_OUTER_BOUND ( 'NONE', #26738, .T. ) ;
#45091=ORIENTED_EDGE ( 'NONE', *, *, #20549, .T. ) ;
#45092=LINE ( 'NONE', #133492, #23684 ) ;
#45093=CARTESIAN_POINT ( 'NONE',  ( -24.29974487139158867, -27.71228299555223273, 4.000000000000000000 ) ) ;
#45094=VECTOR ( 'NONE', #60219, 1000.000000000000227 ) ;
#45095=FACE_OUTER_BOUND ( 'NONE', #20084, .T. ) ;
#45097=DIRECTION ( 'NONE',  ( 0.6830127018922180770, -0.6830127018922204085, -0.2588190451025213501 ) ) ;
#45098=FACE_OUTER_BOUND ( 'NONE', #32750, .T. ) ;
#45100=ORIENTED_EDGE ( 'NONE', *, *, #123572, .T. ) ;
#45101=ORIENTED_EDGE ( 'NONE', *, *, #93098, .T. ) ;
#45102=VERTEX_POINT ( 'NONE', #72927 ) ;
#45103=ORIENTED_EDGE ( 'NONE', *, *, #67773, .T. ) ;
#45104=PLANE ( 'NONE',  #112139 ) ;
#45105=DIRECTION ( 'NONE',  ( 0.6830127018922181881, 0.6830127018922202975, -0.2588190451025214056 ) ) ;
#45106=ORIENTED_EDGE ( 'NONE', *, *, #30038, .T. ) ;
#45107=ORIENTED_EDGE ( 'NONE', *, *, #86562, .T. ) ;
#45108=CARTESIAN_POINT ( 'NONE',  ( -29.99999999999979039, 19.55218569542897100, 5.000000000000000000 ) ) ;
#45110=VERTEX_POINT ( 'NONE', #59872 ) ;
#45112=LINE ( 'NONE', #34202, #39812 ) ;
#45113=VECTOR ( 'NONE', #103093, 1000.000000000000227 ) ;
#45115=FACE_OUTER_BOUND ( 'NONE', #123447, .T. ) ;
#45118=VECTOR ( 'NONE', #106074, 1000.000000000000000 ) ;
#45119=PLANE ( 'NONE',  #46685 ) ;
#45120=PLANE ( 'NONE',  #85825 ) ;
#45121=ADVANCED_FACE ( 'NONE', ( #39561 ), #105486, .F. ) ;
#45123=LINE ( 'NONE', #91453, #68106 ) ;
#45124=VERTEX_POINT ( 'NONE', #138867 ) ;
#45125=CARTESIAN_POINT ( 'NONE',  ( 11.99999999999992006, -0.2811185226894198363, -5.995736974527541285 ) ) ;
#45126=ORIENTED_EDGE ( 'NONE', *, *, #57976, .F. ) ;
#45128=CARTESIAN_POINT ( 'NONE',  ( -33.18398860626899705, 28.73617430169810305, 5.000000000000000000 ) ) ;
#45130=ORIENTED_EDGE ( 'NONE', *, *, #50669, .T. ) ;
#45131=DIRECTION ( 'NONE',  ( -0.7071067811865486830, -0.7071067811865464625, 0.000000000000000000 ) ) ;
#45133=LINE ( 'NONE', #132118, #106608 ) ;
#45134=CARTESIAN_POINT ( 'NONE',  ( 16.49999999999989697, 16.08746187583907528, 4.000000000000000000 ) ) ;
#45135=EDGE_LOOP ( 'NONE', ( #112926, #120526, #50655, #2142 ) ) ;
#45136=LINE ( 'NONE', #130704, #56284 ) ;
#45137=ORIENTED_EDGE ( 'NONE', *, *, #102350, .T. ) ;
#45139=EDGE_CURVE ( 'NONE', #123479, #83438, #79886, .T. ) ;
#45140=CARTESIAN_POINT ( 'NONE',  ( -34.92500000000001137, 22.22500000000000142, 4.000000000000000000 ) ) ;
#45141=EDGE_LOOP ( 'NONE', ( #108603, #135497, #37567 ) ) ;
#45143=ORIENTED_EDGE ( 'NONE', *, *, #57914, .T. ) ;
#45145=DIRECTION ( 'NONE',  ( -0.000000000000000000, -0.3543493200069152693, 0.9351131265310292928 ) ) ;
#45147=AXIS2_PLACEMENT_3D ( 'NONE', #88072, #35142, #44611 ) ;
#45148=LINE ( 'NONE', #122652, #73778 ) ;
#45149=VECTOR ( 'NONE', #54891, 1000.000000000000227 ) ;
#45151=DIRECTION ( 'NONE',  ( 0.3543493200069162685, -0.000000000000000000, -0.9351131265310288487 ) ) ;
#45152=VERTEX_POINT ( 'NONE', #48266 ) ;
#45153=ADVANCED_FACE ( 'NONE', ( #93198 ), #92465, .F. ) ;
#45156=LINE ( 'NONE', #123418, #137297 ) ;
#45157=CARTESIAN_POINT ( 'NONE',  ( 0.000000000000000000, 0.000000000000000000, 5.000000000000000000 ) ) ;
#45159=DIRECTION ( 'NONE',  ( -0.6830127018922180770, -0.6830127018922204085, -0.2588190451025213501 ) ) ;
#45160=EDGE_CURVE ( 'NONE', #97544, #60323, #15592, .T. ) ;
#45161=ORIENTED_EDGE ( 'NONE', *, *, #105669, .T. ) ;
#45162=VERTEX_POINT ( 'NONE', #5450 ) ;
#45164=ORIENTED_EDGE ( 'NONE', *, *, #66902, .T. ) ;
#45165=ORIENTED_EDGE ( 'NONE', *, *, #95420, .F. ) ;
#45167=CARTESIAN_POINT ( 'NONE',  ( 24.42327845806339326, 11.25929247661560950, 17.85071094206578834 ) ) ;
#45169=EDGE_LOOP ( 'NONE', ( #10730, #120333, #70263 ) ) ;
#45170=DIRECTION ( 'NONE',  ( 0.7071067811865487940, 0.7071067811865463515, 0.000000000000000000 ) ) ;
#45171=DIRECTION ( 'NONE',  ( 0.6830127018922181881, 0.6830127018922202975, -0.2588190451025214056 ) ) ;
#45172=CARTESIAN_POINT ( 'NONE',  ( 48.48921356237309510, -27.52281430457089328, 5.000000000000000000 ) ) ;
#45175=ORIENTED_EDGE ( 'NONE', *, *, #65517, .T. ) ;
#45176=CARTESIAN_POINT ( 'NONE',  ( 23.59118151920504047, -0.6989376001503817548, 4.102600482792097658 ) ) ;
#45177=LINE ( 'NONE', #133586, #12147 ) ;
#45178=EDGE_CURVE ( 'NONE', #132084, #48450, #93908, .T. ) ;
#45180=LINE ( 'NONE', #124126, #20134 ) ;
#45181=CARTESIAN_POINT ( 'NONE',  ( 13.82816939922343380, -17.24070752338410628, 4.000000000000000000 ) ) ;
#45182=PLANE ( 'NONE',  #517 ) ;
#45186=DIRECTION ( 'NONE',  ( 0.7071067811865487940, 0.7071067811865463515, -0.000000000000000000 ) ) ;
#45188=VERTEX_POINT ( 'NONE', #141719 ) ;
#45190=LINE ( 'NONE', #34278, #23142 ) ;
#45191=ADVANCED_FACE ( 'NONE', ( #129385 ), #64158, .F. ) ;
#45192=DIRECTION ( 'NONE',  ( -0.7071067811865487940, 0.7071067811865463515, -0.000000000000000000 ) ) ;
#45195=FACE_OUTER_BOUND ( 'NONE', #55406, .T. ) ;
#45196=ADVANCED_FACE ( 'NONE', ( #75749 ), #140283, .F. ) ;
#45197=EDGE_CURVE ( 'NONE', #20616, #32716, #53251, .T. ) ;
#45199=EDGE_LOOP ( 'NONE', ( #73053, #98214, #59926, #28155 ) ) ;
#45201=ORIENTED_EDGE ( 'NONE', *, *, #70594, .F. ) ;
#45202=ORIENTED_EDGE ( 'NONE', *, *, #96029, .F. ) ;
#45204=EDGE_CURVE ( 'NONE', #49135, #115415, #85891, .T. ) ;
#45205=LINE ( 'NONE', #25544, #26879 ) ;
#45207=LINE ( 'NONE', #133616, #48741 ) ;
#45209=EDGE_CURVE ( 'NONE', #94410, #102769, #108318, .T. ) ;
#45210=CARTESIAN_POINT ( 'NONE',  ( -11.96912906347995964, 22.22500000000000142, 13.69883763336573956 ) ) ;
#45211=EDGE_LOOP ( 'NONE', ( #34619, #17767, #16126, #94499 ) ) ;
#45212=DIRECTION ( 'NONE',  ( -0.3543493200069162685, -0.000000000000000000, -0.9351131265310288487 ) ) ;
#45213=ADVANCED_FACE ( 'NONE', ( #86634 ), #132293, .F. ) ;
#45214=CARTESIAN_POINT ( 'NONE',  ( 34.92499999999998295, -13.27521306008087265, -8.452357796116183764 ) ) ;
#45215=CARTESIAN_POINT ( 'NONE',  ( 21.70710678118638270, -18.74070752338409562, 5.000000000000000000 ) ) ;
#45216=DIRECTION ( 'NONE',  ( 0.7071067811865487940, 0.7071067811865463515, 0.000000000000000000 ) ) ;
#45217=DIRECTION ( 'NONE',  ( -0.7071067811865487940, 0.7071067811865463515, -0.000000000000000000 ) ) ;
#45220=EDGE_LOOP ( 'NONE', ( #39815, #50237, #26015, #74769 ) ) ;
#45221=EDGE_CURVE ( 'NONE', #111354, #41615, #21356, .T. ) ;
#45222=DIRECTION ( 'NONE',  ( 0.7071067811865486830, -0.7071067811865464625, -0.000000000000000000 ) ) ;
#45226=CARTESIAN_POINT ( 'NONE',  ( -36.12147316337124892, -20.24070752338407786, 7.412974875817872622 ) ) ;
#45227=CARTESIAN_POINT ( 'NONE',  ( 3.707106781186518152, -0.7407075233842788098, 5.000000000000000000 ) ) ;
#45231=VERTEX_POINT ( 'NONE', #98896 ) ;
#45232=VECTOR ( 'NONE', #40664, 1000.000000000000000 ) ;
#45233=LINE ( 'NONE', #133639, #79298 ) ;
#45234=EDGE_LOOP ( 'NONE', ( #104902, #20270, #130324, #92052 ) ) ;
#45235=CARTESIAN_POINT ( 'NONE',  ( 36.18398860626899705, 28.73617430169812437, 5.000000000000000000 ) ) ;
#45236=CARTESIAN_POINT ( 'NONE',  ( -1.499999999999990896, 6.277155672890267546, -3.510561720658938345 ) ) ;
#45237=DIRECTION ( 'NONE',  ( -0.7071067811865486830, 0.7071067811865464625, 0.000000000000000000 ) ) ;
#45238=FACE_BOUND ( 'NONE', #62926, .T. ) ;
#45240=CARTESIAN_POINT ( 'NONE',  ( -1.828169399223509517, -8.240707523384196875, 4.000000000000000000 ) ) ;
#45241=CARTESIAN_POINT ( 'NONE',  ( -6.005480084712508493, 28.92564299267933947, 4.000000000000000000 ) ) ;
#45242=CARTESIAN_POINT ( 'NONE',  ( -6.489213562373093325, -27.52281430457059841, 5.000000000000000000 ) ) ;
#45243=LINE ( 'NONE', #13974, #71287 ) ;
#45244=ORIENTED_EDGE ( 'NONE', *, *, #1344, .T. ) ;
#45245=LINE ( 'NONE', #2375, #37043 ) ;
#45246=AXIS2_PLACEMENT_3D ( 'NONE', #93473, #72479, #5715 ) ;
#45247=EDGE_LOOP ( 'NONE', ( #70137, #140532, #25537, #51567 ) ) ;
#45249=AXIS2_PLACEMENT_3D ( 'NONE', #52548, #65620, #54716 ) ;
#45250=ADVANCED_FACE ( 'NONE', ( #63471 ), #8989, .F. ) ;
#45251=VECTOR ( 'NONE', #7129, 1000.000000000000000 ) ;
#45252=ORIENTED_EDGE ( 'NONE', *, *, #71492, .F. ) ;
#45254=ORIENTED_EDGE ( 'NONE', *, *, #12537, .F. ) ;
#45255=LINE ( 'NONE', #55392, #140218 ) ;
#45256=AXIS2_PLACEMENT_3D ( 'NONE', #62197, #128172, #17247 ) ;
#45257=LINE ( 'NONE', #91578, #31 ) ;
#45258=AXIS2_PLACEMENT_3D ( 'NONE', #18739, #93475, #28223 ) ;
#45259=VERTEX_POINT ( 'NONE', #118513 ) ;
#45260=DIRECTION ( 'NONE',  ( 0.7071067811865486830, -0.7071067811865464625, -0.000000000000000000 ) ) ;
#45261=CARTESIAN_POINT ( 'NONE',  ( 34.92499999999998295, -15.18334561358938650, 4.500000000000000888 ) ) ;
#45262=LINE ( 'NONE', #89432, #27562 ) ;
#45263=CARTESIAN_POINT ( 'NONE',  ( -24.55388970886357569, 5.485012786255876627, 4.000000000000000000 ) ) ;
#45264=FACE_OUTER_BOUND ( 'NONE', #122544, .T. ) ;
#45265=FACE_OUTER_BOUND ( 'NONE', #124709, .T. ) ;
#45268=LINE ( 'NONE', #13282, #2185 ) ;
#45269=ORIENTED_EDGE ( 'NONE', *, *, #75218, .F. ) ;
#45271=CARTESIAN_POINT ( 'NONE',  ( 0.005480084712502889671, 28.92564299267938210, 4.000000000000000000 ) ) ;
#45273=ORIENTED_EDGE ( 'NONE', *, *, #93574, .F. ) ;
#45274=VERTEX_POINT ( 'NONE', #32980 ) ;
#45275=ORIENTED_EDGE ( 'NONE', *, *, #79206, .F. ) ;
#45277=ORIENTED_EDGE ( 'NONE', *, *, #124002, .T. ) ;
#45278=CARTESIAN_POINT ( 'NONE',  ( -4.954842266633313841, -21.74070752338406720, 21.72585301388583545 ) ) ;
#45279=CARTESIAN_POINT ( 'NONE',  ( -8.994519915287490619, 28.92564299267944250, 4.000000000000000000 ) ) ;
#45282=ORIENTED_EDGE ( 'NONE', *, *, #120883, .F. ) ;
#45283=FACE_OUTER_BOUND ( 'NONE', #29644, .T. ) ;
#45284=DIRECTION ( 'NONE',  ( -0.7071067811865486830, -0.7071067811865464625, 0.000000000000000000 ) ) ;
#45285=EDGE_CURVE ( 'NONE', #63651, #60942, #41678, .T. ) ;
#45286=CARTESIAN_POINT ( 'NONE',  ( -42.48921356237308800, -27.52281430457085065, 5.000000000000000000 ) ) ;
#45287=CARTESIAN_POINT ( 'NONE',  ( 5.999999999999963585, 20.70535890316561733, 1.956823837851902725 ) ) ;
#45288=EDGE_LOOP ( 'NONE', ( #113363, #26446, #49355, #34148 ) ) ;
#45289=EDGE_LOOP ( 'NONE', ( #86805, #27282, #112791, #102263 ) ) ;
#45290=DIRECTION ( 'NONE',  ( 0.6830127018922180770, -0.6830127018922204085, -0.2588190451025213501 ) ) ;
#45291=CARTESIAN_POINT ( 'NONE',  ( -6.707013264292997157, -21.74070752338405654, 4.999753212805220670 ) ) ;
#45292=DIRECTION ( 'NONE',  ( 1.000000000000000000, 0.000000000000000000, 0.000000000000000000 ) ) ;
#45293=EDGE_LOOP ( 'NONE', ( #52535, #47046, #39990, #16077 ) ) ;
#45294=DIRECTION ( 'NONE',  ( -0.000000000000000000, -0.3543493200069152693, 0.9351131265310292928 ) ) ;
#45295=FACE_OUTER_BOUND ( 'NONE', #58846, .T. ) ;
#45297=ADVANCED_FACE ( 'NONE', ( #117769 ), #96727, .T. ) ;
#45298=CARTESIAN_POINT ( 'NONE',  ( 18.48921356237309510, -27.52281430457068367, 5.000000000000000000 ) ) ;
#45299=LINE ( 'NONE', #2438, #30163 ) ;
#45301=LINE ( 'NONE', #2441, #32370 ) ;
#45303=PLANE ( 'NONE',  #97723 ) ;
#45304=ADVANCED_FACE ( 'NONE', ( #106921 ), #62741, .T. ) ;
#45307=EDGE_CURVE ( 'NONE', #18576, #17742, #130128, .T. ) ;
#45308=EDGE_CURVE ( 'NONE', #17086, #119805, #31523, .T. ) ;
#45309=EDGE_LOOP ( 'NONE', ( #135620, #37231, #32717, #94170 ) ) ;
#45310=ORIENTED_EDGE ( 'NONE', *, *, #121060, .F. ) ;
#45312=CARTESIAN_POINT ( 'NONE',  ( 0.2997448713915885632, -27.71228299555206220, 4.000000000000000000 ) ) ;
#45313=ADVANCED_FACE ( 'NONE', ( #67007 ), #35113, .F. ) ;
#45314=EDGE_CURVE ( 'NONE', #124953, #142228, #112645, .T. ) ;
#45315=AXIS2_PLACEMENT_3D ( 'NONE', #124323, #36591, #93129 ) ;
#45316=CARTESIAN_POINT ( 'NONE',  ( 42.48921356237308800, -27.52281430457085065, 5.000000000000000000 ) ) ;
#45317=VERTEX_POINT ( 'NONE', #68466 ) ;
#45318=LINE ( 'NONE', #124976, #32251 ) ;
#45319=DIRECTION ( 'NONE',  ( 0.7071067811865487940, -0.7071067811865463515, 0.000000000000000000 ) ) ;
#45320=PLANE ( 'NONE',  #21257 ) ;
#45322=EDGE_CURVE ( 'NONE', #34296, #90987, #55422, .T. ) ;
#45324=DIRECTION ( 'NONE',  ( -0.7071067811865486830, -0.7071067811865464625, 0.000000000000000000 ) ) ;
#45325=CARTESIAN_POINT ( 'NONE',  ( 21.00548008471250938, 28.92564299267923644, 4.000000000000000000 ) ) ;
#45326=DIRECTION ( 'NONE',  ( -0.000000000000000000, -0.3543493200069152693, 0.9351131265310292928 ) ) ;
#45328=CARTESIAN_POINT ( 'NONE',  ( 27.66846741159839596, -18.74070752338408852, 20.73178291233847759 ) ) ;
#45329=ADVANCED_FACE ( 'NONE', ( #35841 ), #1696, .T. ) ;
#45330=CARTESIAN_POINT ( 'NONE',  ( -36.70679250724052167, 20.25929247661551358, 20.83292124670823142 ) ) ;
#45331=VECTOR ( 'NONE', #32473, 1000.000000000000227 ) ;
#45333=DIRECTION ( 'NONE',  ( 0.7071067811865487940, 0.7071067811865463515, 0.000000000000000000 ) ) ;
#45334=ORIENTED_EDGE ( 'NONE', *, *, #130924, .F. ) ;
#45336=VERTEX_POINT ( 'NONE', #46737 ) ;
#45337=LINE ( 'NONE', #34421, #126477 ) ;
#45338=EDGE_CURVE ( 'NONE', #139251, #32532, #13307, .T. ) ;
#45339=LINE ( 'NONE', #89515, #115540 ) ;
#45341=CARTESIAN_POINT ( 'NONE',  ( -6.328169399223488867, -15.74070752338412049, 4.000000000000000000 ) ) ;
#45342=LINE ( 'NONE', #22791, #83452 ) ;
#45343=FACE_OUTER_BOUND ( 'NONE', #50844, .T. ) ;
#45346=CARTESIAN_POINT ( 'NONE',  ( 22.49999999999984368, 21.43112307739195899, 4.000000000000000000 ) ) ;
#45347=CARTESIAN_POINT ( 'NONE',  ( 27.70710678118635428, -9.740707523384186217, 5.000000000000000000 ) ) ;
#45348=EDGE_CURVE ( 'NONE', #47525, #67739, #80059, .T. ) ;
#45349=PLANE ( 'NONE',  #126121 ) ;
#45350=VECTOR ( 'NONE', #112735, 999.9999999999998863 ) ;
#45351=CARTESIAN_POINT ( 'NONE',  ( 32.99999999999976552, -18.03360074219755660, 5.000000000000000000 ) ) ;
#45353=CARTESIAN_POINT ( 'NONE',  ( -34.92500000000001137, -10.29806943317888290, 4.500000000000000888 ) ) ;
#45354=VECTOR ( 'NONE', #101130, 1000.000000000000227 ) ;
#45355=CARTESIAN_POINT ( 'NONE',  ( -24.29974487139158867, -27.71228299555223273, 4.000000000000000000 ) ) ;
#45356=VERTEX_POINT ( 'NONE', #24220 ) ;
#45360=DIRECTION ( 'NONE',  ( 0.7071067811865487940, 0.7071067811865463515, 0.000000000000000000 ) ) ;
#45361=CARTESIAN_POINT ( 'NONE',  ( -1.499999999999982236, 1.087461875839230707, 4.000000000000000000 ) ) ;
#45362=EDGE_CURVE ( 'NONE', #62795, #61349, #57578, .T. ) ;
#45363=EDGE_LOOP ( 'NONE', ( #126870, #4460, #113928, #109288 ) ) ;
#45364=CARTESIAN_POINT ( 'NONE',  ( -13.11017322888201697, -22.22500000000000142, 4.785647885939352975 ) ) ;
#45365=EDGE_CURVE ( 'NONE', #95876, #141613, #14023, .T. ) ;
#45368=ADVANCED_FACE ( 'NONE', ( #58324 ), #77197, .F. ) ;
#45370=ORIENTED_EDGE ( 'NONE', *, *, #1841, .T. ) ;
#45372=EDGE_CURVE ( 'NONE', #129322, #58187, #102505, .T. ) ;
#45373=CARTESIAN_POINT ( 'NONE',  ( -8.207106781186476852, -20.24070752338407075, 5.000000000000000000 ) ) ;
#45375=CARTESIAN_POINT ( 'NONE',  ( -32.99999999999977263, -5.527737879153217015, -7.983877177622296095 ) ) ;
#45376=PLANE ( 'NONE',  #76686 ) ;
#45377=CARTESIAN_POINT ( 'NONE',  ( 34.47516574401890921, -8.971932658884092859, 4.998110765256834398 ) ) ;
#45378=ORIENTED_EDGE ( 'NONE', *, *, #796, .T. ) ;
#45381=LINE ( 'NONE', #60537, #14715 ) ;
#45382=EDGE_LOOP ( 'NONE', ( #47256, #139651, #54873, #112587 ) ) ;
#45383=ORIENTED_EDGE ( 'NONE', *, *, #79569, .F. ) ;
#45386=ADVANCED_FACE ( 'NONE', ( #124235 ), #24912, .F. ) ;
#45389=CARTESIAN_POINT ( 'NONE',  ( 4.171830600776436526, -5.240707523384232402, 4.000000000000000000 ) ) ;
#45390=DIRECTION ( 'NONE',  ( -0.7071067811865486830, 0.7071067811865464625, 0.000000000000000000 ) ) ;
#45391=DIRECTION ( 'NONE',  ( 0.7071067811865487940, -0.7071067811865463515, 0.000000000000000000 ) ) ;
#45392=ORIENTED_EDGE ( 'NONE', *, *, #42451, .F. ) ;
#45393=VERTEX_POINT ( 'NONE', #100353 ) ;
#45394=DIRECTION ( 'NONE',  ( -0.7071067811865486830, -0.7071067811865464625, 0.000000000000000000 ) ) ;
#45396=ADVANCED_FACE ( 'NONE', ( #110477 ), #79354, .F. ) ;
#45397=ORIENTED_EDGE ( 'NONE', *, *, #19721, .F. ) ;
#45398=LINE ( 'NONE', #80865, #106862 ) ;
#45399=CARTESIAN_POINT ( 'NONE',  ( 24.48921356237309510, -27.52281430457072631, 5.000000000000000000 ) ) ;
#45400=FACE_OUTER_BOUND ( 'NONE', #18903, .T. ) ;
#45401=( BOUNDED_CURVE ( )  B_SPLINE_CURVE ( 3, ( #86745, #109904, #54140, #65741 ),
 .UNSPECIFIED., .F., .T. ) 
 B_SPLINE_CURVE_WITH_KNOTS ( ( 4, 4 ),
 ( 1.964434688349488756, 3.503810798801452187 ),
 .UNSPECIFIED. ) 
 CURVE ( )  GEOMETRIC_REPRESENTATION_ITEM ( )  RATIONAL_B_SPLINE_CURVE ( ( 1.000000000000000000, 0.8120851936182280628, 0.8120851936182280628, 1.000000000000000000 ) ) 
 REPRESENTATION_ITEM ( '' )  );
#45402=ORIENTED_EDGE ( 'NONE', *, *, #35365, .T. ) ;
#45403=EDGE_CURVE ( 'NONE', #13716, #82359, #1004, .T. ) ;
#45404=FACE_BOUND ( 'NONE', #119233, .T. ) ;
#45405=DIRECTION ( 'NONE',  ( -0.3543493200069163240, -0.000000000000000000, 0.9351131265310288487 ) ) ;
#45406=DIRECTION ( 'NONE',  ( 1.000000000000000000, 0.000000000000000000, 0.000000000000000000 ) ) ;
#45407=CARTESIAN_POINT ( 'NONE',  ( 38.99451991528749062, 28.92564299267965211, 4.000000000000000000 ) ) ;
#45408=DIRECTION ( 'NONE',  ( -0.7071067811865486830, -0.7071067811865464625, 0.000000000000000000 ) ) ;
#45409=CARTESIAN_POINT ( 'NONE',  ( -20.29298673570681544, -21.74070752338406720, 4.999753212805217117 ) ) ;
#45411=VECTOR ( 'NONE', #138179, 1000.000000000000000 ) ;
#45412=ORIENTED_EDGE ( 'NONE', *, *, #138260, .F. ) ;
#45413=EDGE_CURVE ( 'NONE', #47758, #126555, #121369, .T. ) ;
#45414=VERTEX_POINT ( 'NONE', #11145 ) ;
#45416=ORIENTED_EDGE ( 'NONE', *, *, #38912, .T. ) ;
#45420=CARTESIAN_POINT ( 'NONE',  ( -23.20710678118638981, 18.75929247661553134, 5.000000000000000000 ) ) ;
#45421=EDGE_CURVE ( 'NONE', #68681, #123983, #44579, .T. ) ;
#45423=CARTESIAN_POINT ( 'NONE',  ( -29.29289321881324426, -0.7407075233842805861, 5.000000000000000000 ) ) ;
#45424=EDGE_CURVE ( 'NONE', #36667, #90206, #33683, .T. ) ;
#45425=VERTEX_POINT ( 'NONE', #90168 ) ;
#45426=LINE ( 'NONE', #13444, #122357 ) ;
#45427=DIRECTION ( 'NONE',  ( 1.000000000000000000, 0.000000000000000000, 0.000000000000000000 ) ) ;
#45428=LINE ( 'NONE', #78745, #105579 ) ;
#45431=DIRECTION ( 'NONE',  ( -0.7071067811865486830, -0.7071067811865464625, 0.000000000000000000 ) ) ;
#45432=DIRECTION ( 'NONE',  ( -0.000000000000000000, 0.000000000000000000, 1.000000000000000000 ) ) ;
#45433=EDGE_LOOP ( 'NONE', ( #20651, #52885, #142082, #5577 ) ) ;
#45435=DIRECTION ( 'NONE',  ( 0.7071067811865487940, 0.7071067811865463515, 0.000000000000000000 ) ) ;
#45436=VERTEX_POINT ( 'NONE', #116923 ) ;
#45437=ORIENTED_EDGE ( 'NONE', *, *, #137379, .F. ) ;
#45438=EDGE_CURVE ( 'NONE', #6138, #131532, #60440, .T. ) ;
#45441=ORIENTED_EDGE ( 'NONE', *, *, #15169, .T. ) ;
#45442=VECTOR ( 'NONE', #37331, 1000.000000000000227 ) ;
#45443=LINE ( 'NONE', #108481, #60561 ) ;
#45448=ORIENTED_EDGE ( 'NONE', *, *, #128837, .F. ) ;
#45449=VECTOR ( 'NONE', #116817, 1000.000000000000227 ) ;
#45451=DIRECTION ( 'NONE',  ( 1.000000000000000000, -0.000000000000000000, 0.000000000000000000 ) ) ;
#45452=VECTOR ( 'NONE', #87030, 1000.000000000000000 ) ;
#45453=CARTESIAN_POINT ( 'NONE',  ( 27.18398860626900060, 28.73617430169806042, 5.000000000000000000 ) ) ;
#45454=ORIENTED_EDGE ( 'NONE', *, *, #29816, .F. ) ;
#45456=DIRECTION ( 'NONE',  ( 0.7071067811865487940, 0.7071067811865463515, -0.000000000000000000 ) ) ;
#45457=LINE ( 'NONE', #22216, #45149 ) ;
#45458=ORIENTED_EDGE ( 'NONE', *, *, #120231, .T. ) ;
#45459=CARTESIAN_POINT ( 'NONE',  ( 15.18398860626900237, 28.73617430169797871, 5.000000000000000000 ) ) ;
#45460=VERTEX_POINT ( 'NONE', #93034 ) ;
#45461=ORIENTED_EDGE ( 'NONE', *, *, #24186, .T. ) ;
#45462=EDGE_LOOP ( 'NONE', ( #119272, #135019, #80609, #112207 ) ) ;
#45463=EDGE_CURVE ( 'NONE', #91901, #91730, #37228, .T. ) ;
#45464=CARTESIAN_POINT ( 'NONE',  ( 36.83652871126526662, 15.75929247661555799, 9.299976744543005935 ) ) ;
#45465=DIRECTION ( 'NONE',  ( -0.7071067811865487940, 0.7071067811865463515, -0.000000000000000000 ) ) ;
#45466=LINE ( 'NONE', #67193, #64843 ) ;
#45467=EDGE_CURVE ( 'NONE', #63778, #40456, #59035, .T. ) ;
#45468=ADVANCED_FACE ( 'NONE', ( #106017 ), #71302, .T. ) ;
#45470=DIRECTION ( 'NONE',  ( -0.000000000000000000, 0.000000000000000000, 1.000000000000000000 ) ) ;
#45471=ORIENTED_EDGE ( 'NONE', *, *, #47305, .T. ) ;
#45472=CARTESIAN_POINT ( 'NONE',  ( 28.82816939922333432, -20.24070752338407431, 4.000000000000000000 ) ) ;
#45474=EDGE_CURVE ( 'NONE', #35947, #59015, #15430, .T. ) ;
#45476=CARTESIAN_POINT ( 'NONE',  ( -3.717577386425651831, -21.73023691814492153, 5.000000000000000888 ) ) ;
#45477=ADVANCED_FACE ( 'NONE', ( #105328 ), #27771, .T. ) ;
#45478=CARTESIAN_POINT ( 'NONE',  ( -23.48860328114998453, 7.166961737892989071, 4.667035327419722712 ) ) ;
#45479=CARTESIAN_POINT ( 'NONE',  ( -14.20710678118644665, -2.240707523384257716, 5.000000000000000000 ) ) ;
#45480=ORIENTED_EDGE ( 'NONE', *, *, #241, .F. ) ;
#45482=EDGE_CURVE ( 'NONE', #74460, #20468, #137979, .T. ) ;
#45483=EDGE_LOOP ( 'NONE', ( #13245, #11015, #31659, #33871 ) ) ;
#45486=VECTOR ( 'NONE', #128765, 1000.000000000000227 ) ;
#45487=EDGE_CURVE ( 'NONE', #65559, #20866, #138700, .T. ) ;
#45488=DIRECTION ( 'NONE',  ( -0.6830127018922181881, 0.6830127018922202975, -0.2588190451025214056 ) ) ;
#45489=DIRECTION ( 'NONE',  ( 0.7071067811865487940, -0.7071067811865463515, 0.000000000000000000 ) ) ;
#45491=ADVANCED_FACE ( 'NONE', ( #36515 ), #5282, .T. ) ;
#45492=LINE ( 'NONE', #78812, #108505 ) ;
#45493=DIRECTION ( 'NONE',  ( -0.7071067811865487940, 0.7071067811865463515, -0.000000000000000000 ) ) ;
#45494=FACE_OUTER_BOUND ( 'NONE', #86329, .T. ) ;
#45495=DIRECTION ( 'NONE',  ( -0.7071067811865486830, -0.7071067811865464625, 0.000000000000000000 ) ) ;
#45496=ORIENTED_EDGE ( 'NONE', *, *, #112737, .F. ) ;
#45498=VECTOR ( 'NONE', #65676, 999.9999999999998863 ) ;
#45499=ORIENTED_EDGE ( 'NONE', *, *, #72582, .F. ) ;
#45502=EDGE_CURVE ( 'NONE', #57842, #19888, #116215, .T. ) ;
#45504=CARTESIAN_POINT ( 'NONE',  ( 2.588385094051668833, 22.22500000000000497, 4.777194822843813249 ) ) ;
#45505=ORIENTED_EDGE ( 'NONE', *, *, #109920, .F. ) ;
#45506=FACE_OUTER_BOUND ( 'NONE', #122523, .T. ) ;
#45507=PLANE ( 'NONE',  #21736 ) ;
#45508=ORIENTED_EDGE ( 'NONE', *, *, #31211, .F. ) ;
#45509=ORIENTED_EDGE ( 'NONE', *, *, #71165, .T. ) ;
#45510=DIRECTION ( 'NONE',  ( -0.6830127018922180770, -0.6830127018922204085, -0.2588190451025213501 ) ) ;
#45511=VERTEX_POINT ( 'NONE', #16146 ) ;
#45512=ADVANCED_FACE ( 'NONE', ( #38661 ), #48834, .T. ) ;
#45513=LINE ( 'NONE', #78842, #56628 ) ;
#45516=CARTESIAN_POINT ( 'NONE',  ( -72.18398860626899705, 28.73617430169837661, 5.000000000000000000 ) ) ;
#45518=EDGE_LOOP ( 'NONE', ( #72040, #95000, #61316, #96930 ) ) ;
#45519=VECTOR ( 'NONE', #80342, 1000.000000000000227 ) ;
#45520=PLANE ( 'NONE',  #79218 ) ;
#45521=CARTESIAN_POINT ( 'NONE',  ( 24.29974487139158867, -27.71228299555223273, 4.000000000000000000 ) ) ;
#45522=LINE ( 'NONE', #3382, #80848 ) ;
#45525=CARTESIAN_POINT ( 'NONE',  ( -48.29974487139158867, -27.71228299555239971, 4.000000000000000000 ) ) ;
#45526=DIRECTION ( 'NONE',  ( -0.3543493200069162685, -0.000000000000000000, -0.9351131265310288487 ) ) ;
#45527=ORIENTED_EDGE ( 'NONE', *, *, #5245, .F. ) ;
#45528=VERTEX_POINT ( 'NONE', #124941 ) ;
#45529=CARTESIAN_POINT ( 'NONE',  ( 34.92499999999998295, 15.58119340046983758, 2.482413320905456633 ) ) ;
#45531=ORIENTED_EDGE ( 'NONE', *, *, #126232, .F. ) ;
#45532=VECTOR ( 'NONE', #22182, 999.9999999999998863 ) ;
#45534=EDGE_CURVE ( 'NONE', #142960, #42538, #26358, .T. ) ;
#45535=DIRECTION ( 'NONE',  ( -0.7071067811865487940, 0.7071067811865463515, 0.000000000000000000 ) ) ;
#45536=CARTESIAN_POINT ( 'NONE',  ( -7.828169399223478209, 0.7592924766157120864, 4.000000000000000000 ) ) ;
#45537=FACE_OUTER_BOUND ( 'NONE', #67666, .T. ) ;
#45539=ORIENTED_EDGE ( 'NONE', *, *, #88420, .T. ) ;
#45541=DIRECTION ( 'NONE',  ( -0.7071067811865487940, 0.7071067811865463515, 0.000000000000000000 ) ) ;
#45542=EDGE_CURVE ( 'NONE', #11127, #116312, #53077, .T. ) ;
#45545=CARTESIAN_POINT ( 'NONE',  ( 1.499999999999990896, 22.01701374228155927, 2.453858888625627621 ) ) ;
#45546=DIRECTION ( 'NONE',  ( -0.000000000000000000, 0.000000000000000000, 1.000000000000000000 ) ) ;
#45548=EDGE_LOOP ( 'NONE', ( #44884, #95530, #36299 ) ) ;
#45549=CARTESIAN_POINT ( 'NONE',  ( -54.18398860626899705, 28.73617430169825226, 5.000000000000000000 ) ) ;
#45550=PLANE ( 'NONE',  #141926 ) ;
#45551=DIRECTION ( 'NONE',  ( 0.7071067811865487940, -0.7071067811865463515, 0.000000000000000000 ) ) ;
#45552=ADVANCED_FACE ( 'NONE', ( #85707 ), #42958, .T. ) ;
#45553=VECTOR ( 'NONE', #17865, 999.9999999999998863 ) ;
#45554=CARTESIAN_POINT ( 'NONE',  ( 39.18398860626899705, 28.73617430169814568, 5.000000000000000000 ) ) ;
#45556=EDGE_LOOP ( 'NONE', ( #17106, #100205, #69141, #142626 ) ) ;
#45557=EDGE_LOOP ( 'NONE', ( #31399, #105204, #38714, #60340, #101373 ) ) ;
#45558=ORIENTED_EDGE ( 'NONE', *, *, #133692, .T. ) ;
#45559=VECTOR ( 'NONE', #112401, 1000.000000000000000 ) ;
#45561=ORIENTED_EDGE ( 'NONE', *, *, #36282, .F. ) ;
#45562=EDGE_CURVE ( 'NONE', #11291, #125242, #32061, .T. ) ;
#45563=CARTESIAN_POINT ( 'NONE',  ( 9.299744871391588674, -27.71228299555212971, 4.000000000000000000 ) ) ;
#45564=LINE ( 'NONE', #132573, #126663 ) ;
#45565=PLANE ( 'NONE',  #64259 ) ;
#45566=VECTOR ( 'NONE', #107549, 1000.000000000000000 ) ;
#45567=CARTESIAN_POINT ( 'NONE',  ( -17.20710678118642889, 18.75929247661552779, 5.000000000000000000 ) ) ;
#45568=ORIENTED_EDGE ( 'NONE', *, *, #14906, .T. ) ;
#45569=LINE ( 'NONE', #110746, #37486 ) ;
#45571=CARTESIAN_POINT ( 'NONE',  ( 19.49999999999986500, 14.14708470758592895, -0.5283514160167009921 ) ) ;
#45573=ORIENTED_EDGE ( 'NONE', *, *, #82015, .F. ) ;
#45574=EDGE_CURVE ( 'NONE', #39797, #57666, #29901, .T. ) ;
#45575=CARTESIAN_POINT ( 'NONE',  ( 42.18398860626899705, 28.73617430169816700, 5.000000000000000000 ) ) ;
#45577=VERTEX_POINT ( 'NONE', #64697 ) ;
#45578=VERTEX_POINT ( 'NONE', #41497 ) ;
#45579=EDGE_CURVE ( 'NONE', #58696, #645, #131380, .T. ) ;
#45580=DIRECTION ( 'NONE',  ( 1.000000000000000000, 0.000000000000000000, 0.000000000000000000 ) ) ;
#45582=LINE ( 'NONE', #133984, #18757 ) ;
#45584=CARTESIAN_POINT ( 'NONE',  ( -16.49999999999987566, 13.46639925780212010, 5.000000000000000000 ) ) ;
#45586=ADVANCED_FACE ( 'NONE', ( #76293 ), #128531, .F. ) ;
#45588=ORIENTED_EDGE ( 'NONE', *, *, #44198, .F. ) ;
#45589=PLANE ( 'NONE',  #57337 ) ;
#45590=VERTEX_POINT ( 'NONE', #63302 ) ;
#45591=ORIENTED_EDGE ( 'NONE', *, *, #105987, .F. ) ;
#45592=VECTOR ( 'NONE', #48554, 1000.000000000000000 ) ;
#45593=ADVANCED_FACE ( 'NONE', ( #7426 ), #120449, .F. ) ;
#45594=LINE ( 'NONE', #12203, #40473 ) ;
#45595=ADVANCED_FACE ( 'NONE', ( #53836 ), #129951, .F. ) ;
#45598=CARTESIAN_POINT ( 'NONE',  ( -15.18398860626900237, 28.73617430169797871, 5.000000000000000000 ) ) ;
#45599=VECTOR ( 'NONE', #82079, 1000.000000000000000 ) ;
#45600=CARTESIAN_POINT ( 'NONE',  ( 1.499999999999994449, 13.56627193232215056, -10.57019076586068351 ) ) ;
#45601=CARTESIAN_POINT ( 'NONE',  ( 17.67183060077635304, 11.25929247661560950, 4.000000000000000000 ) ) ;
#45602=EDGE_LOOP ( 'NONE', ( #62768, #126009, #43986, #10858 ) ) ;
#45603=CARTESIAN_POINT ( 'NONE',  ( -42.48921356237308800, -27.52281430457085065, 5.000000000000000000 ) ) ;
#45606=DIRECTION ( 'NONE',  ( -0.6830127018922181881, 0.6830127018922202975, -0.2588190451025214056 ) ) ;
#45607=ORIENTED_EDGE ( 'NONE', *, *, #88392, .T. ) ;
#45608=DIRECTION ( 'NONE',  ( -0.7071067811865486830, -0.7071067811865464625, 0.000000000000000000 ) ) ;
#45609=EDGE_CURVE ( 'NONE', #114228, #81908, #119058, .T. ) ;
#45610=ORIENTED_EDGE ( 'NONE', *, *, #13763, .F. ) ;
#45611=CARTESIAN_POINT ( 'NONE',  ( -45.48921356237309510, -27.52281430457087197, 5.000000000000000000 ) ) ;
#45612=ORIENTED_EDGE ( 'NONE', *, *, #57881, .T. ) ;
#45614=VERTEX_POINT ( 'NONE', #107472 ) ;
#45616=CARTESIAN_POINT ( 'NONE',  ( 8.538396446294241215, -9.740707523384180888, 17.74957260769612688 ) ) ;
#45617=DIRECTION ( 'NONE',  ( 0.3543493200069162685, -0.000000000000000000, -0.9351131265310288487 ) ) ;
#45618=CARTESIAN_POINT ( 'NONE',  ( 6.183988606268994381, 28.73617430169791476, 5.000000000000000000 ) ) ;
#45619=VECTOR ( 'NONE', #106871, 999.9999999999998863 ) ;
#45621=DIRECTION ( 'NONE',  ( -0.000000000000000000, 0.000000000000000000, 1.000000000000000000 ) ) ;
#45622=LINE ( 'NONE', #134035, #87569 ) ;
#45623=CARTESIAN_POINT ( 'NONE',  ( 2.700255128608413990, -27.71228299555204089, 4.000000000000000000 ) ) ;
#45624=VERTEX_POINT ( 'NONE', #139434 ) ;
#45625=CARTESIAN_POINT ( 'NONE',  ( 12.29974487139158512, -27.71228299555214747, 4.000000000000000000 ) ) ;
#45626=DIRECTION ( 'NONE',  ( 0.7071067811865487940, 0.7071067811865463515, 0.000000000000000000 ) ) ;
#45627=DIRECTION ( 'NONE',  ( -0.000000000000000000, 0.000000000000000000, 1.000000000000000000 ) ) ;
#45629=ORIENTED_EDGE ( 'NONE', *, *, #46855, .F. ) ;
#45630=EDGE_CURVE ( 'NONE', #137150, #20442, #10290, .T. ) ;
#45631=CARTESIAN_POINT ( 'NONE',  ( -10.59167451900992418, -0.7407075233842735917, 14.76736230305378328 ) ) ;
#45632=ORIENTED_EDGE ( 'NONE', *, *, #13588, .F. ) ;
#45633=ORIENTED_EDGE ( 'NONE', *, *, #52250, .F. ) ;
#45634=DIRECTION ( 'NONE',  ( 0.7071067811865486830, -0.7071067811865464625, -0.000000000000000000 ) ) ;
#45635=CARTESIAN_POINT ( 'NONE',  ( 29.99999999999979039, -12.41253812416062985, 4.000000000000000000 ) ) ;
#45636=DIRECTION ( 'NONE',  ( -0.000000000000000000, 0.3543493200069153248, 0.9351131265310292928 ) ) ;
#45637=LINE ( 'NONE', #122436, #2399 ) ;
#45638=ORIENTED_EDGE ( 'NONE', *, *, #24812, .F. ) ;
#45639=DIRECTION ( 'NONE',  ( -0.7071067811865486830, -0.7071067811865464625, 0.000000000000000000 ) ) ;
#45640=ORIENTED_EDGE ( 'NONE', *, *, #24705, .T. ) ;
#45641=VECTOR ( 'NONE', #32179, 1000.000000000000000 ) ;
#45642=VECTOR ( 'NONE', #141473, 1000.000000000000000 ) ;
#45643=DIRECTION ( 'NONE',  ( -0.7071067811865487940, 0.7071067811865463515, -0.000000000000000000 ) ) ;
#45644=VECTOR ( 'NONE', #17160, 1000.000000000000000 ) ;
#45645=EDGE_CURVE ( 'NONE', #138468, #41591, #84333, .T. ) ;
#45647=ORIENTED_EDGE ( 'NONE', *, *, #103919, .F. ) ;
#45649=EDGE_CURVE ( 'NONE', #81493, #116320, #42247, .T. ) ;
#45650=CARTESIAN_POINT ( 'NONE',  ( -24.32816939922335209, -9.740707523384187994, 4.000000000000000000 ) ) ;
#45651=CARTESIAN_POINT ( 'NONE',  ( 2.700255128608413990, -27.71228299555204089, 4.000000000000000000 ) ) ;
#45652=EDGE_LOOP ( 'NONE', ( #105752, #77221, #95662, #134899, #134801, #70470 ) ) ;
#45653=VECTOR ( 'NONE', #36036, 999.9999999999998863 ) ;
#45654=ORIENTED_EDGE ( 'NONE', *, *, #134174, .F. ) ;
#45655=EDGE_CURVE ( 'NONE', #142129, #39099, #106741, .T. ) ;
#45656=VERTEX_POINT ( 'NONE', #8136 ) ;
#45657=CARTESIAN_POINT ( 'NONE',  ( 11.67183060077639034, 8.259292476615637923, 4.000000000000000000 ) ) ;
#45658=PLANE ( 'NONE',  #9212 ) ;
#45660=VECTOR ( 'NONE', #135749, 1000.000000000000000 ) ;
#45661=CARTESIAN_POINT ( 'NONE',  ( -21.18398860626899349, 28.73617430169802134, 5.000000000000000000 ) ) ;
#45662=EDGE_CURVE ( 'NONE', #106288, #42560, #86458, .T. ) ;
#45663=FACE_OUTER_BOUND ( 'NONE', #115166, .T. ) ;
#45664=VERTEX_POINT ( 'NONE', #75577 ) ;
#45666=ADVANCED_FACE ( 'NONE', ( #129214 ), #118337, .F. ) ;
#45667=DIRECTION ( 'NONE',  ( 1.000000000000000000, 0.000000000000000000, 0.000000000000000000 ) ) ;
#45669=ORIENTED_EDGE ( 'NONE', *, *, #70549, .F. ) ;
#45670=LINE ( 'NONE', #11541, #113744 ) ;
#45671=DIRECTION ( 'NONE',  ( 0.000000000000000000, -1.000000000000000000, 0.000000000000000000 ) ) ;
#45672=VERTEX_POINT ( 'NONE', #44398 ) ;
#45673=EDGE_CURVE ( 'NONE', #103418, #57341, #66139, .T. ) ;
#45674=DIRECTION ( 'NONE',  ( 0.6830127018922180770, -0.6830127018922204085, -0.2588190451025213501 ) ) ;
#45675=EDGE_LOOP ( 'NONE', ( #56305, #51589, #114979, #56302 ) ) ;
#45676=VERTEX_POINT ( 'NONE', #99429 ) ;
#45677=EDGE_CURVE ( 'NONE', #109576, #15478, #24746, .T. ) ;
#45678=LINE ( 'NONE', #110164, #84061 ) ;
#45680=AXIS2_PLACEMENT_3D ( 'NONE', #13464, #104042, #136693 ) ;
#45681=VERTEX_POINT ( 'NONE', #13845 ) ;
#45682=EDGE_CURVE ( 'NONE', #14544, #41659, #21890, .T. ) ;
#45683=CARTESIAN_POINT ( 'NONE',  ( 9.183988606268997046, 28.73617430169793607, 5.000000000000000000 ) ) ;
#45684=LINE ( 'NONE', #114459, #143431 ) ;
#45685=VECTOR ( 'NONE', #66256, 999.9999999999998863 ) ;
#45686=CARTESIAN_POINT ( 'NONE',  ( 11.81601139373100651, 28.73617430169779041, 5.000000000000000000 ) ) ;
#45687=DIRECTION ( 'NONE',  ( 0.7071067811865487940, -0.7071067811865463515, -0.000000000000000000 ) ) ;
#45688=CARTESIAN_POINT ( 'NONE',  ( 34.92499999999998295, 5.718490437204210686, 4.759050581649325373 ) ) ;
#45689=LINE ( 'NONE', #66012, #97685 ) ;
#45690=DIRECTION ( 'NONE',  ( -0.000000000000000000, 0.3543493200069153248, 0.9351131265310292928 ) ) ;
#45691=DIRECTION ( 'NONE',  ( 0.7071067811865486830, -0.7071067811865464625, -0.000000000000000000 ) ) ;
#45695=DIRECTION ( 'NONE',  ( -0.000000000000000000, 0.000000000000000000, 1.000000000000000000 ) ) ;
#45697=FACE_OUTER_BOUND ( 'NONE', #54491, .T. ) ;
#45698=VERTEX_POINT ( 'NONE', #68992 ) ;
#45699=ORIENTED_EDGE ( 'NONE', *, *, #96121, .F. ) ;
#45701=EDGE_LOOP ( 'NONE', ( #53530, #33993, #80741, #138084 ) ) ;
#45702=ORIENTED_EDGE ( 'NONE', *, *, #138003, .F. ) ;
#45703=ORIENTED_EDGE ( 'NONE', *, *, #31052, .T. ) ;
#45704=EDGE_CURVE ( 'NONE', #130345, #61667, #100184, .T. ) ;
#45705=PLANE ( 'NONE',  #119725 ) ;
#45706=DIRECTION ( 'NONE',  ( 0.6830127018922181881, 0.6830127018922202975, -0.2588190451025214056 ) ) ;
#45707=DIRECTION ( 'NONE',  ( 0.7071067811865487940, -0.7071067811865463515, 0.000000000000000000 ) ) ;
#45709=CARTESIAN_POINT ( 'NONE',  ( -33.48921356237309510, -27.52281430457078670, 5.000000000000000000 ) ) ;
#45710=DIRECTION ( 'NONE',  ( -0.3543493200069162685, -0.000000000000000000, -0.9351131265310288487 ) ) ;
#45711=DIRECTION ( 'NONE',  ( -0.000000000000000000, 0.000000000000000000, 1.000000000000000000 ) ) ;
#45712=VECTOR ( 'NONE', #49866, 1000.000000000000114 ) ;
#45713=CARTESIAN_POINT ( 'NONE',  ( -7.499999999999951150, 1.030536316426505117, -5.498701923753780640 ) ) ;
#45714=ORIENTED_EDGE ( 'NONE', *, *, #99183, .F. ) ;
#45715=DIRECTION ( 'NONE',  ( -0.7071067811865486830, -0.7071067811865464625, 0.000000000000000000 ) ) ;
#45716=DIRECTION ( 'NONE',  ( 0.7071067811865486830, -0.7071067811865464625, -0.000000000000000000 ) ) ;
#45717=DIRECTION ( 'NONE',  ( -0.000000000000000000, 0.3543493200069153248, 0.9351131265310292928 ) ) ;
#45720=LINE ( 'NONE', #57310, #33085 ) ;
#45721=DIRECTION ( 'NONE',  ( 0.7071067811865486830, -0.7071067811865464625, -0.000000000000000000 ) ) ;
#45722=CARTESIAN_POINT ( 'NONE',  ( 5.007369047664765205, 22.22500000000000142, -10.13186738250296592 ) ) ;
#45723=EDGE_CURVE ( 'NONE', #123521, #81380, #45816, .T. ) ;
#45724=DIRECTION ( 'NONE',  ( 0.000000000000000000, -0.3543493200069153248, -0.9351131265310291818 ) ) ;
#45725=ORIENTED_EDGE ( 'NONE', *, *, #62000, .T. ) ;
#45726=ORIENTED_EDGE ( 'NONE', *, *, #94664, .T. ) ;
#45729=AXIS2_PLACEMENT_3D ( 'NONE', #84055, #128253, #73168 ) ;
#45730=ORIENTED_EDGE ( 'NONE', *, *, #5304, .F. ) ;
#45731=ADVANCED_FACE ( 'NONE', ( #46559 ), #68305, .F. ) ;
#45733=CARTESIAN_POINT ( 'NONE',  ( 34.49999999999976552, -13.91253812416061386, 4.000000000000000000 ) ) ;
#45734=CARTESIAN_POINT ( 'NONE',  ( -45.18398860626900415, 28.73617430169818832, 5.000000000000000000 ) ) ;
#45735=DIRECTION ( 'NONE',  ( 0.7071067811865487940, 0.7071067811865463515, 0.000000000000000000 ) ) ;
#45737=ORIENTED_EDGE ( 'NONE', *, *, #130130, .T. ) ;
#45738=EDGE_CURVE ( 'NONE', #28591, #123227, #134975, .T. ) ;
#45740=LINE ( 'NONE', #102252, #45559 ) ;
#45741=ORIENTED_EDGE ( 'NONE', *, *, #58155, .F. ) ;
#45742=VERTEX_POINT ( 'NONE', #1533 ) ;
#45743=VECTOR ( 'NONE', #25032, 1000.000000000000227 ) ;
#45746=VERTEX_POINT ( 'NONE', #79176 ) ;
#45747=CARTESIAN_POINT ( 'NONE',  ( 0.000000000000000000, -21.72500000000000142, 4.500000000000000888 ) ) ;
#45749=APPLICATION_CONTEXT ( 'automotive_design' ) ;
#45751=VECTOR ( 'NONE', #90514, 999.9999999999998863 ) ;
#45752=VECTOR ( 'NONE', #76787, 1000.000000000000000 ) ;
#45753=AXIS2_PLACEMENT_3D ( 'NONE', #30555, #50165, #28411 ) ;
#45755=ORIENTED_EDGE ( 'NONE', *, *, #34171, .F. ) ;
#45756=LINE ( 'NONE', #20379, #89585 ) ;
#45757=ORIENTED_EDGE ( 'NONE', *, *, #35692, .F. ) ;
#45760=ORIENTED_EDGE ( 'NONE', *, *, #116995, .F. ) ;
#45763=ADVANCED_FACE ( 'NONE', ( #77721 ), #90747, .F. ) ;
#45764=ORIENTED_EDGE ( 'NONE', *, *, #83500, .T. ) ;
#45765=DIRECTION ( 'NONE',  ( 0.7071067811865487940, 0.7071067811865463515, 0.000000000000000000 ) ) ;
#45766=EDGE_CURVE ( 'NONE', #108133, #39160, #24045, .T. ) ;
#45767=DIRECTION ( 'NONE',  ( -0.7071067811865487940, 0.7071067811865463515, -0.000000000000000000 ) ) ;
#45769=CARTESIAN_POINT ( 'NONE',  ( -29.99999999999979039, 10.55218569542906515, 5.000000000000000000 ) ) ;
#45771=FACE_BOUND ( 'NONE', #31703, .T. ) ;
#45772=EDGE_LOOP ( 'NONE', ( #91944, #71207, #25325, #124038 ) ) ;
#45773=CARTESIAN_POINT ( 'NONE',  ( 0.4368010322082955810, -12.74070752338415247, 9.898150129686374754 ) ) ;
#45774=CARTESIAN_POINT ( 'NONE',  ( -48.18398860626899705, 28.73617430169820608, 5.000000000000000000 ) ) ;
#45776=PLANE ( 'NONE',  #60128 ) ;
#45777=EDGE_CURVE ( 'NONE', #131756, #141782, #33520, .T. ) ;
#45778=ORIENTED_EDGE ( 'NONE', *, *, #80473, .T. ) ;
#45779=DIRECTION ( 'NONE',  ( 0.7071067811865487940, 0.7071067811865463515, -0.000000000000000000 ) ) ;
#45780=ORIENTED_EDGE ( 'NONE', *, *, #36466, .T. ) ;
#45781=VECTOR ( 'NONE', #101760, 1000.000000000000000 ) ;
#45782=EDGE_LOOP ( 'NONE', ( #127325, #71299, #64164, #16160 ) ) ;
#45783=ORIENTED_EDGE ( 'NONE', *, *, #71746, .T. ) ;
#45785=AXIS2_PLACEMENT_3D ( 'NONE', #4924, #28162, #136200 ) ;
#45786=ORIENTED_EDGE ( 'NONE', *, *, #128627, .F. ) ;
#45787=CARTESIAN_POINT ( 'NONE',  ( -42.18398860626899705, 28.73617430169816700, 5.000000000000000000 ) ) ;
#45789=EDGE_LOOP ( 'NONE', ( #43456, #118962, #59201, #107713 ) ) ;
#45790=EDGE_CURVE ( 'NONE', #69258, #129048, #66837, .T. ) ;
#45792=LINE ( 'NONE', #68969, #59780 ) ;
#45793=CARTESIAN_POINT ( 'NONE',  ( 27.51665438641025219, 22.22500000000000142, 4.500000000000000888 ) ) ;
#45794=CARTESIAN_POINT ( 'NONE',  ( 11.51078643762690490, -27.52281430457047406, 5.000000000000000000 ) ) ;
#45795=ORIENTED_EDGE ( 'NONE', *, *, #141042, .T. ) ;
#45796=ORIENTED_EDGE ( 'NONE', *, *, #135121, .F. ) ;
#45797=VERTEX_POINT ( 'NONE', #121196 ) ;
#45798=ORIENTED_EDGE ( 'NONE', *, *, #134438, .F. ) ;
#45799=CARTESIAN_POINT ( 'NONE',  ( 24.00548008471250938, 28.92564299267921513, 4.000000000000000000 ) ) ;
#45800=VERTEX_POINT ( 'NONE', #34210 ) ;
#45801=ORIENTED_EDGE ( 'NONE', *, *, #921, .T. ) ;
#45803=LINE ( 'NONE', #100865, #43946 ) ;
#45805=CARTESIAN_POINT ( 'NONE',  ( -6.489213562373093325, -27.52281430457059841, 5.000000000000000000 ) ) ;
#45806=DIRECTION ( 'NONE',  ( -0.7071067811865486830, -0.7071067811865464625, 0.000000000000000000 ) ) ;
#45808=EDGE_CURVE ( 'NONE', #48333, #54912, #10982, .T. ) ;
#45810=ORIENTED_EDGE ( 'NONE', *, *, #33335, .T. ) ;
#45812=VECTOR ( 'NONE', #136672, 1000.000000000000000 ) ;
#45813=EDGE_CURVE ( 'NONE', #89147, #29105, #56718, .T. ) ;
#45814=CARTESIAN_POINT ( 'NONE',  ( 3.489213562373097322, -27.52281430457057709, 5.000000000000000000 ) ) ;
#45815=CARTESIAN_POINT ( 'NONE',  ( 26.99999999999981526, -6.033600742197678279, 5.000000000000000000 ) ) ;
#45816=LINE ( 'NONE', #23296, #70401 ) ;
#45817=DIRECTION ( 'NONE',  ( -0.7071067811865487940, 0.7071067811865463515, -0.000000000000000000 ) ) ;
#45818=VERTEX_POINT ( 'NONE', #100879 ) ;
#45819=LINE ( 'NONE', #68308, #13785 ) ;
#45820=EDGE_LOOP ( 'NONE', ( #101466, #143115, #60997, #89371 ) ) ;
#45821=LINE ( 'NONE', #55990, #105233 ) ;
#45822=DIRECTION ( 'NONE',  ( -0.7071067811865486830, 0.7071067811865464625, 0.000000000000000000 ) ) ;
#45823=ADVANCED_FACE ( 'NONE', ( #111770 ), #50091, .F. ) ;
#45824=EDGE_CURVE ( 'NONE', #19198, #2249, #49399, .T. ) ;
#45827=PLANE ( 'NONE',  #18123 ) ;
#45828=VECTOR ( 'NONE', #48722, 999.9999999999998863 ) ;
#45829=LINE ( 'NONE', #99441, #14110 ) ;
#45830=LINE ( 'NONE', #77034, #56036 ) ;
#45831=ORIENTED_EDGE ( 'NONE', *, *, #23726, .F. ) ;
#45832=VECTOR ( 'NONE', #39569, 999.9999999999998863 ) ;
#45833=DIRECTION ( 'NONE',  ( -0.000000000000000000, 0.3543493200069153248, 0.9351131265310292928 ) ) ;
#45834=ORIENTED_EDGE ( 'NONE', *, *, #128356, .F. ) ;
#45836=ADVANCED_FACE ( 'NONE', ( #16726 ), #61004, .F. ) ;
#45837=CARTESIAN_POINT ( 'NONE',  ( 36.48921356237310221, -27.52281430457080802, 5.000000000000000000 ) ) ;
#45838=CARTESIAN_POINT ( 'NONE',  ( -17.99999999999986855, -22.06887692260758271, 4.000000000000000000 ) ) ;
#45840=EDGE_CURVE ( 'NONE', #142336, #21645, #124776, .T. ) ;
#45841=EDGE_LOOP ( 'NONE', ( #104120, #30803, #37032, #80737 ) ) ;
#45843=LINE ( 'NONE', #66161, #119987 ) ;
#45844=VECTOR ( 'NONE', #135805, 1000.000000000000000 ) ;
#45846=VECTOR ( 'NONE', #93536, 1000.000000000000000 ) ;
#45847=ADVANCED_FACE ( 'NONE', ( #47968 ), #116022, .T. ) ;
#45848=DIRECTION ( 'NONE',  ( -0.7071067811865487940, 0.7071067811865463515, -0.000000000000000000 ) ) ;
#45849=CARTESIAN_POINT ( 'NONE',  ( -12.79289321881336861, -5.240707523384230626, 5.000000000000000000 ) ) ;
#45850=ORIENTED_EDGE ( 'NONE', *, *, #116671, .T. ) ;
#45851=LINE ( 'NONE', #89329, #48957 ) ;
#45852=CARTESIAN_POINT ( 'NONE',  ( 34.49999999999976552, 7.464255608400424791, 4.994342998332163219 ) ) ;
#45853=DIRECTION ( 'NONE',  ( 0.7071067811865487940, 0.7071067811865463515, 0.000000000000000000 ) ) ;
#45855=PLANE ( 'NONE',  #77148 ) ;
#45856=CARTESIAN_POINT ( 'NONE',  ( -34.60428828362105236, 22.19175015946030882, 4.000000000000000000 ) ) ;
#45859=ORIENTED_EDGE ( 'NONE', *, *, #46794, .F. ) ;
#45860=ORIENTED_EDGE ( 'NONE', *, *, #115687, .F. ) ;
#45861=CARTESIAN_POINT ( 'NONE',  ( -30.29974487139158867, -27.71228299555227537, 4.000000000000000000 ) ) ;
#45862=ORIENTED_EDGE ( 'NONE', *, *, #85471, .F. ) ;
#45863=ORIENTED_EDGE ( 'NONE', *, *, #115572, .F. ) ;
#45864=ORIENTED_EDGE ( 'NONE', *, *, #120732, .T. ) ;
#45865=EDGE_CURVE ( 'NONE', #104944, #47327, #83431, .T. ) ;
#45866=DIRECTION ( 'NONE',  ( -0.3543493200069162685, -0.000000000000000000, -0.9351131265310288487 ) ) ;
#45867=CARTESIAN_POINT ( 'NONE',  ( -33.48921356237309510, -27.52281430457078670, 5.000000000000000000 ) ) ;
#45868=ORIENTED_EDGE ( 'NONE', *, *, #80379, .T. ) ;
#45870=DIRECTION ( 'NONE',  ( -0.000000000000000000, -0.3543493200069152693, 0.9351131265310292928 ) ) ;
#45871=PLANE ( 'NONE',  #122741 ) ;
#45872=CARTESIAN_POINT ( 'NONE',  ( 19.49999999999987210, 21.05218569542895679, 5.000000000000000000 ) ) ;
#45875=EDGE_CURVE ( 'NONE', #45317, #22333, #38493, .T. ) ;
#45876=LINE ( 'NONE', #133585, #55781 ) ;
#45877=CARTESIAN_POINT ( 'NONE',  ( 14.29298673570684919, -21.74070752338406365, 4.999753212805221558 ) ) ;
#45878=VECTOR ( 'NONE', #29693, 1000.000000000000000 ) ;
#45879=CARTESIAN_POINT ( 'NONE',  ( 12.66846741159848655, -18.74070752338408852, 20.73178291233844206 ) ) ;
#45881=DIRECTION ( 'NONE',  ( 0.7071067811865487940, 0.7071067811865463515, 0.000000000000000000 ) ) ;
#45883=DIRECTION ( 'NONE',  ( -0.6830127018922180770, -0.6830127018922204085, -0.2588190451025213501 ) ) ;
#45885=ADVANCED_FACE ( 'NONE', ( #27590 ), #104438, .F. ) ;
#45886=CARTESIAN_POINT ( 'NONE',  ( 12.48921356237309155, -27.52281430457064104, 5.000000000000000000 ) ) ;
#45887=CARTESIAN_POINT ( 'NONE',  ( 48.18398860626899705, 28.73617430169820608, 5.000000000000000000 ) ) ;
#45888=ORIENTED_EDGE ( 'NONE', *, *, #108913, .F. ) ;
#45889=ORIENTED_EDGE ( 'NONE', *, *, #78473, .F. ) ;
#45891=CARTESIAN_POINT ( 'NONE',  ( -34.49999999999975842, -10.53574439159939757, 4.994342998332166772 ) ) ;
#45892=ORIENTED_EDGE ( 'NONE', *, *, #49283, .F. ) ;
#45893=CARTESIAN_POINT ( 'NONE',  ( 24.18398860626899705, 28.73617430169804265, 5.000000000000000000 ) ) ;
#45894=CARTESIAN_POINT ( 'NONE',  ( -2.700255128608413990, -27.71228299555204089, 4.000000000000000000 ) ) ;
#45897=ORIENTED_EDGE ( 'NONE', *, *, #1571, .T. ) ;
#45898=CARTESIAN_POINT ( 'NONE',  ( 16.82816939922340183, -20.24070752338408852, 4.000000000000000000 ) ) ;
#45900=CARTESIAN_POINT ( 'NONE',  ( 36.48921356237310221, -27.52281430457080802, 5.000000000000000000 ) ) ;
#45901=PLANE ( 'NONE',  #100871 ) ;
#45902=CARTESIAN_POINT ( 'NONE',  ( 10.73493329717942224, 12.75929247661558286, 18.34774599283953833 ) ) ;
#45903=FACE_OUTER_BOUND ( 'NONE', #118897, .T. ) ;
#45904=ORIENTED_EDGE ( 'NONE', *, *, #13836, .F. ) ;
#45905=PLANE ( 'NONE',  #53484 ) ;
#45906=EDGE_CURVE ( 'NONE', #100067, #116077, #138518, .T. ) ;
#45907=ORIENTED_EDGE ( 'NONE', *, *, #29937, .T. ) ;
#45909=FACE_OUTER_BOUND ( 'NONE', #131081, .T. ) ;
#45910=DIRECTION ( 'NONE',  ( -0.7071067811865486830, -0.7071067811865464625, 0.000000000000000000 ) ) ;
#45911=FACE_OUTER_BOUND ( 'NONE', #111371, .T. ) ;
#45912=LINE ( 'NONE', #90096, #115704 ) ;
#45913=CARTESIAN_POINT ( 'NONE',  ( 33.29974487139158867, -27.71228299555229313, 4.000000000000000000 ) ) ;
#45914=EDGE_LOOP ( 'NONE', ( #43527, #128009, #1470, #32141 ) ) ;
#45915=VECTOR ( 'NONE', #4498, 1000.000000000000000 ) ;
#45916=LINE ( 'NONE', #87970, #124035 ) ;
#45918=MANIFOLD_SOLID_BREP ( 'Mirror1', #23189 ) ;
#45919=CARTESIAN_POINT ( 'NONE',  ( 32.99451991528749062, 28.92564299267960948, 4.000000000000000000 ) ) ;
#45920=LINE ( 'NONE', #90103, #43149 ) ;
#45921=CARTESIAN_POINT ( 'NONE',  ( -62.99451991528749772, 28.92564299267982264, 4.000000000000000000 ) ) ;
#45922=ORIENTED_EDGE ( 'NONE', *, *, #96316, .F. ) ;
#45923=ORIENTED_EDGE ( 'NONE', *, *, #74281, .F. ) ;
#45925=ORIENTED_EDGE ( 'NONE', *, *, #56811, .T. ) ;
#45927=EDGE_LOOP ( 'NONE', ( #78348, #73859, #77452, #10717 ) ) ;
#45929=CARTESIAN_POINT ( 'NONE',  ( -24.18398860626899705, 28.73617430169804265, 5.000000000000000000 ) ) ;
#45930=CARTESIAN_POINT ( 'NONE',  ( 34.92382263987068569, 21.75929247661549937, 4.252424926123345550 ) ) ;
#45933=VECTOR ( 'NONE', #40074, 1000.000000000000000 ) ;
#45934=EDGE_CURVE ( 'NONE', #9641, #16, #48655, .T. ) ;
#45935=FACE_BOUND ( 'NONE', #124543, .T. ) ;
#45936=LINE ( 'NONE', #79309, #47989 ) ;
#45937=CARTESIAN_POINT ( 'NONE',  ( 39.18398860626899705, 28.73617430169814568, 5.000000000000000000 ) ) ;
#45938=DIRECTION ( 'NONE',  ( -0.7071067811865487940, 0.7071067811865463515, 0.000000000000000000 ) ) ;
#45939=ADVANCED_FACE ( 'NONE', ( #82030 ), #126213, .F. ) ;
#45940=LINE ( 'NONE', #88732, #133685 ) ;
#45941=FACE_OUTER_BOUND ( 'NONE', #86823, .T. ) ;
#45942=EDGE_LOOP ( 'NONE', ( #23180, #48254, #70109, #54846 ) ) ;
#45943=VECTOR ( 'NONE', #81271, 1000.000000000000000 ) ;
#45945=PLANE ( 'NONE',  #69579 ) ;
#45946=ORIENTED_EDGE ( 'NONE', *, *, #44329, .T. ) ;
#45947=ORIENTED_EDGE ( 'NONE', *, *, #12926, .F. ) ;
#45950=CARTESIAN_POINT ( 'NONE',  ( -27.48921356237309155, -27.52281430457074762, 5.000000000000000000 ) ) ;
#45951=( BOUNDED_CURVE ( )  B_SPLINE_CURVE ( 3, ( #107289, #7961, #96388, #140626 ),
 .UNSPECIFIED., .F., .T. ) 
 B_SPLINE_CURVE_WITH_KNOTS ( ( 4, 4 ),
 ( 1.964434688349487867, 3.503810798801452187 ),
 .UNSPECIFIED. ) 
 CURVE ( )  GEOMETRIC_REPRESENTATION_ITEM ( )  RATIONAL_B_SPLINE_CURVE ( ( 1.000000000000000000, 0.8120851936182279518, 0.8120851936182279518, 1.000000000000000000 ) ) 
 REPRESENTATION_ITEM ( '' )  );
#45953=CARTESIAN_POINT ( 'NONE',  ( -30.18398860626900060, 28.73617430169808173, 5.000000000000000000 ) ) ;
#45954=VERTEX_POINT ( 'NONE', #95713 ) ;
#45955=DIRECTION ( 'NONE',  ( 0.6830127018922180770, -0.6830127018922204085, -0.2588190451025213501 ) ) ;
#45956=VECTOR ( 'NONE', #96582, 1000.000000000000000 ) ;
#45957=ADVANCED_FACE ( 'NONE', ( #84167 ), #52895, .F. ) ;
#45958=DIRECTION ( 'NONE',  ( -0.000000000000000000, -0.3543493200069152693, 0.9351131265310292928 ) ) ;
#45959=VECTOR ( 'NONE', #25140, 1000.000000000000227 ) ;
#45960=DIRECTION ( 'NONE',  ( -0.000000000000000000, 0.000000000000000000, 1.000000000000000000 ) ) ;
#45962=CARTESIAN_POINT ( 'NONE',  ( -11.29289321881337038, 2.259292476615690770, 5.000000000000000000 ) ) ;
#45963=DIRECTION ( 'NONE',  ( -0.6830127018922180770, -0.6830127018922204085, -0.2588190451025213501 ) ) ;
#45964=DIRECTION ( 'NONE',  ( 0.7071067811865487940, 0.7071067811865463515, 0.000000000000000000 ) ) ;
#45965=CARTESIAN_POINT ( 'NONE',  ( -30.18398860626900060, 28.73617430169808173, 5.000000000000000000 ) ) ;
#45966=VERTEX_POINT ( 'NONE', #20278 ) ;
#45969=ORIENTED_EDGE ( 'NONE', *, *, #5579, .F. ) ;
#45970=LINE ( 'NONE', #55407, #47302 ) ;
#45971=FACE_OUTER_BOUND ( 'NONE', #69733, .T. ) ;
#45972=ORIENTED_EDGE ( 'NONE', *, *, #122528, .F. ) ;
#45973=VECTOR ( 'NONE', #96586, 1000.000000000000000 ) ;
#45974=EDGE_LOOP ( 'NONE', ( #45397, #105567, #25291, #44763 ) ) ;
#45976=VERTEX_POINT ( 'NONE', #42074 ) ;
#45978=ORIENTED_EDGE ( 'NONE', *, *, #4183, .T. ) ;
#45979=CARTESIAN_POINT ( 'NONE',  ( 59.99451991528749772, 28.92564299267980132, 4.000000000000000000 ) ) ;
#45980=( BOUNDED_CURVE ( )  B_SPLINE_CURVE ( 3, ( #89298, #111767, #134972, #35671 ),
 .UNSPECIFIED., .F., .T. ) 
 B_SPLINE_CURVE_WITH_KNOTS ( ( 4, 4 ),
 ( 1.208578181583240374, 1.359146454359417167 ),
 .UNSPECIFIED. ) 
 CURVE ( )  GEOMETRIC_REPRESENTATION_ITEM ( )  RATIONAL_B_SPLINE_CURVE ( ( 1.000000000000000000, 0.9981116584018959736, 0.9981116584018959736, 1.000000000000000000 ) ) 
 REPRESENTATION_ITEM ( '' )  );
#45982=LINE ( 'NONE', #134410, #58862 ) ;
#45983=VERTEX_POINT ( 'NONE', #53658 ) ;
#45984=CARTESIAN_POINT ( 'NONE',  ( -25.49999999999982236, -17.91344420646044711, 1.358650452708403567 ) ) ;
#45986=CARTESIAN_POINT ( 'NONE',  ( 26.99999999999981171, -8.731860332648819778, -2.120594902707474638 ) ) ;
#45987=DIRECTION ( 'NONE',  ( -0.6830127018922180770, -0.6830127018922204085, -0.2588190451025213501 ) ) ;
#45988=VECTOR ( 'NONE', #100694, 1000.000000000000227 ) ;
#45989=PLANE ( 'NONE',  #79499 ) ;
#45990=ORIENTED_EDGE ( 'NONE', *, *, #60366, .F. ) ;
#45991=ORIENTED_EDGE ( 'NONE', *, *, #102283, .F. ) ;
#45992=CARTESIAN_POINT ( 'NONE',  ( -15.29974487139158867, -27.71228299555216879, 4.000000000000000000 ) ) ;
#45993=CARTESIAN_POINT ( 'NONE',  ( 27.70710678118635428, -0.7407075233842701500, 5.000000000000000000 ) ) ;
#45995=EDGE_CURVE ( 'NONE', #74781, #141351, #62398, .T. ) ;
#45997=PLANE ( 'NONE',  #74925 ) ;
#45998=EDGE_LOOP ( 'NONE', ( #134977, #117753, #19425, #103752 ) ) ;
#45999=CARTESIAN_POINT ( 'NONE',  ( 0.000000000000000000, 0.000000000000000000, 5.000000000000000000 ) ) ;
#46000=CARTESIAN_POINT ( 'NONE',  ( -3.707106781186518152, 17.25929247661554911, 5.000000000000000000 ) ) ;
#46002=CARTESIAN_POINT ( 'NONE',  ( -39.29974487139159578, -27.71228299555233576, 4.000000000000000000 ) ) ;
#46003=LINE ( 'NONE', #24234, #36914 ) ;
#46005=CARTESIAN_POINT ( 'NONE',  ( 57.48921356237308800, -27.52281430457095368, 5.000000000000000000 ) ) ;
#46006=PLANE ( 'NONE',  #67758 ) ;
#46007=DIRECTION ( 'NONE',  ( -0.3543493200069162685, -0.000000000000000000, -0.9351131265310288487 ) ) ;
#46010=ORIENTED_EDGE ( 'NONE', *, *, #44690, .F. ) ;
#46011=EDGE_CURVE ( 'NONE', #45672, #132598, #41322, .T. ) ;
#46012=EDGE_LOOP ( 'NONE', ( #88172, #116868, #127477, #71038 ) ) ;
#46014=PLANE ( 'NONE',  #12298 ) ;
#46015=DIRECTION ( 'NONE',  ( 0.6830127018922181881, 0.6830127018922202975, -0.2588190451025214056 ) ) ;
#46017=ORIENTED_EDGE ( 'NONE', *, *, #57302, .F. ) ;
#46018=CARTESIAN_POINT ( 'NONE',  ( 7.966599676569728672, 6.759292476615653023, 12.28218704918523940 ) ) ;
#46019=FACE_OUTER_BOUND ( 'NONE', #71014, .T. ) ;
#46020=EDGE_CURVE ( 'NONE', #41843, #92431, #107987, .T. ) ;
#46021=DIRECTION ( 'NONE',  ( 0.7071067811865487940, 0.7071067811865463515, 0.000000000000000000 ) ) ;
#46023=PLANE ( 'NONE',  #156 ) ;
#46025=CARTESIAN_POINT ( 'NONE',  ( -65.99451991528749772, 28.92564299267984396, 4.000000000000000000 ) ) ;
#46026=EDGE_CURVE ( 'NONE', #74278, #113076, #17435, .T. ) ;
#46027=CARTESIAN_POINT ( 'NONE',  ( -5.207106781186502609, 9.759292476615618384, 5.000000000000000000 ) ) ;
#46029=PLANE ( 'NONE',  #4685 ) ;
#46030=CARTESIAN_POINT ( 'NONE',  ( -8.510786437626906675, -27.52281430457049183, 5.000000000000000000 ) ) ;
#46031=VECTOR ( 'NONE', #106569, 1000.000000000000000 ) ;
#46033=VERTEX_POINT ( 'NONE', #84843 ) ;
#46035=ORIENTED_EDGE ( 'NONE', *, *, #106820, .F. ) ;
#46036=ADVANCED_FACE ( 'NONE', ( #7971 ), #105851, .F. ) ;
#46037=DIRECTION ( 'NONE',  ( 0.3543493200069163240, -0.000000000000000000, 0.9351131265310288487 ) ) ;
#46039=VECTOR ( 'NONE', #115654, 1000.000000000000000 ) ;
#46040=VECTOR ( 'NONE', #93521, 1000.000000000000000 ) ;
#46041=CARTESIAN_POINT ( 'NONE',  ( -42.18398860626899705, 28.73617430169816700, 5.000000000000000000 ) ) ;
#46042=LINE ( 'NONE', #122130, #81315 ) ;
#46043=AXIS2_PLACEMENT_3D ( 'NONE', #79841, #14536, #103647 ) ;
#46044=CARTESIAN_POINT ( 'NONE',  ( -24.51665438641027706, 22.22500000000000142, 4.500000000000000888 ) ) ;
#46045=DIRECTION ( 'NONE',  ( -0.7071067811865486830, -0.7071067811865464625, -0.000000000000000000 ) ) ;
#46046=LINE ( 'NONE', #33043, #1379 ) ;
#46047=EDGE_LOOP ( 'NONE', ( #112397, #49809, #61956, #2330, #94452 ) ) ;
#46048=ORIENTED_EDGE ( 'NONE', *, *, #75371, .T. ) ;
#46049=DIRECTION ( 'NONE',  ( -0.6830127018922180770, -0.6830127018922204085, -0.2588190451025213501 ) ) ;
#46053=AXIS2_PLACEMENT_3D ( 'NONE', #82961, #80833, #4603 ) ;
#46054=CARTESIAN_POINT ( 'NONE',  ( 24.32816939922335564, 20.25929247661551003, 4.000000000000000000 ) ) ;
#46055=DIRECTION ( 'NONE',  ( -0.7071067811865486830, -0.7071067811865464625, 0.000000000000000000 ) ) ;
#46060=CARTESIAN_POINT ( 'NONE',  ( -69.18398860626899705, 28.73617430169835529, 5.000000000000000000 ) ) ;
#46063=DIRECTION ( 'NONE',  ( 0.7071067811865486830, -0.7071067811865464625, -0.000000000000000000 ) ) ;
#46064=DIRECTION ( 'NONE',  ( 0.3543493200069162685, -0.000000000000000000, -0.9351131265310288487 ) ) ;
#46066=VECTOR ( 'NONE', #59409, 1000.000000000000000 ) ;
#46067=VERTEX_POINT ( 'NONE', #128365 ) ;
#46068=ADVANCED_FACE ( 'NONE', ( #18857 ), #52211, .T. ) ;
#46069=CARTESIAN_POINT ( 'NONE',  ( 12.18398860626900060, 28.73617430169795739, 5.000000000000000000 ) ) ;
#46070=VECTOR ( 'NONE', #43902, 1000.000000000000000 ) ;
#46073=VECTOR ( 'NONE', #124815, 999.9999999999998863 ) ;
#46074=EDGE_LOOP ( 'NONE', ( #132471, #44408, #115853, #10137 ) ) ;
#46075=ORIENTED_EDGE ( 'NONE', *, *, #110888, .T. ) ;
#46076=VECTOR ( 'NONE', #90446, 1000.000000000000000 ) ;
#46077=AXIS2_PLACEMENT_3D ( 'NONE', #57087, #101269, #120130 ) ;
#46079=VECTOR ( 'NONE', #51183, 1000.000000000000000 ) ;
#46080=FACE_OUTER_BOUND ( 'NONE', #76813, .T. ) ;
#46081=LINE ( 'NONE', #34465, #7071 ) ;
#46082=DIRECTION ( 'NONE',  ( 0.6830127018922180770, -0.6830127018922204085, -0.2588190451025213501 ) ) ;
#46083=ORIENTED_EDGE ( 'NONE', *, *, #135014, .F. ) ;
#46084=CARTESIAN_POINT ( 'NONE',  ( -5.510786437626906675, -27.52281430457051314, 5.000000000000000000 ) ) ;
#46085=DIRECTION ( 'NONE',  ( -0.6830127018922181881, 0.6830127018922202975, -0.2588190451025214056 ) ) ;
#46088=CARTESIAN_POINT ( 'NONE',  ( 0.000000000000000000, 0.000000000000000000, 5.000000000000000000 ) ) ;
#46090=ORIENTED_EDGE ( 'NONE', *, *, #115441, .F. ) ;
#46091=ORIENTED_EDGE ( 'NONE', *, *, #25553, .T. ) ;
#46093=ORIENTED_EDGE ( 'NONE', *, *, #109447, .F. ) ;
#46095=LINE ( 'NONE', #133109, #48058 ) ;
#46098=ORIENTED_EDGE ( 'NONE', *, *, #90683, .F. ) ;
#46099=EDGE_LOOP ( 'NONE', ( #101787, #22161, #62448, #2019, #5922 ) ) ;
#46100=VECTOR ( 'NONE', #41699, 1000.000000000000000 ) ;
#46101=LINE ( 'NONE', #1115, #125544 ) ;
#46106=CARTESIAN_POINT ( 'NONE',  ( -57.18398860626899705, 28.73617430169827358, 5.000000000000000000 ) ) ;
#46107=EDGE_LOOP ( 'NONE', ( #141532, #111516, #138566, #136525 ) ) ;
#46108=EDGE_CURVE ( 'NONE', #16056, #9912, #19580, .T. ) ;
#46109=ADVANCED_FACE ( 'NONE', ( #123739 ), #57064, .F. ) ;
#46110=FACE_BOUND ( 'NONE', #87476, .T. ) ;
#46111=CARTESIAN_POINT ( 'NONE',  ( 13.10966639810773948, 3.759292476615678336, 4.164048746910661514 ) ) ;
#46112=CARTESIAN_POINT ( 'NONE',  ( -2.206660635421508143, 21.75929247661549937, 4.998822639870708073 ) ) ;
#46113=DIRECTION ( 'NONE',  ( -0.3543493200069162685, -0.000000000000000000, -0.9351131265310288487 ) ) ;
#46114=CARTESIAN_POINT ( 'NONE',  ( -20.20003122016824548, 8.259292476615634371, 16.85664084051845890 ) ) ;
#46115=EDGE_CURVE ( 'NONE', #25446, #137546, #59212, .T. ) ;
#46116=EDGE_CURVE ( 'NONE', #22881, #18685, #4012, .T. ) ;
#46117=DIRECTION ( 'NONE',  ( -0.6830127018922180770, -0.6830127018922204085, -0.2588190451025213501 ) ) ;
#46119=ORIENTED_EDGE ( 'NONE', *, *, #75287, .T. ) ;
#46120=VERTEX_POINT ( 'NONE', #45472 ) ;
#46123=EDGE_CURVE ( 'NONE', #89522, #74016, #35312, .T. ) ;
#46124=DIRECTION ( 'NONE',  ( 0.7071067811865486830, -0.7071067811865464625, -0.000000000000000000 ) ) ;
#46125=VERTEX_POINT ( 'NONE', #113533 ) ;
#46126=CARTESIAN_POINT ( 'NONE',  ( 78.48921356237309510, -27.52281430457109934, 5.000000000000000000 ) ) ;
#46127=DIRECTION ( 'NONE',  ( -0.000000000000000000, 0.000000000000000000, 1.000000000000000000 ) ) ;
#46129=CARTESIAN_POINT ( 'NONE',  ( -36.29974487139159578, -27.71228299555231445, 4.000000000000000000 ) ) ;
#46130=VERTEX_POINT ( 'NONE', #3336 ) ;
#46131=FACE_OUTER_BOUND ( 'NONE', #47130, .T. ) ;
#46132=CYLINDRICAL_SURFACE ( 'NONE', #17209, 3.378199999999994319 ) ;
#46133=DIRECTION ( 'NONE',  ( -0.6830127018922181881, 0.6830127018922202975, -0.2588190451025214056 ) ) ;
#46134=PLANE ( 'NONE',  #103615 ) ;
#46135=CARTESIAN_POINT ( 'NONE',  ( -2.700255128608413990, -27.71228299555204089, 4.000000000000000000 ) ) ;
#46136=DIRECTION ( 'NONE',  ( 0.7071067811865487940, 0.7071067811865463515, -0.000000000000000000 ) ) ;
#46137=DIRECTION ( 'NONE',  ( -0.7071067811865487940, 0.7071067811865463515, 0.000000000000000000 ) ) ;
#46138=VECTOR ( 'NONE', #58064, 1000.000000000000000 ) ;
#46139=CIRCLE ( 'NONE', #127122, 0.5000000000000000000 ) ;
#46140=EDGE_CURVE ( 'NONE', #119913, #102340, #111394, .T. ) ;
#46142=CARTESIAN_POINT ( 'NONE',  ( -34.92500000000001137, 20.82781275693358225, 4.470553524000292711 ) ) ;
#46143=AXIS2_PLACEMENT_3D ( 'NONE', #20002, #109169, #77298 ) ;
#46144=ORIENTED_EDGE ( 'NONE', *, *, #73202, .T. ) ;
#46145=CARTESIAN_POINT ( 'NONE',  ( 6.005480084712508493, 28.92564299267933947, 4.000000000000000000 ) ) ;
#46146=CARTESIAN_POINT ( 'NONE',  ( 26.99999999999981881, -19.06887692260762179, 4.000000000000000000 ) ) ;
#46148=ORIENTED_EDGE ( 'NONE', *, *, #29379, .T. ) ;
#46149=ORIENTED_EDGE ( 'NONE', *, *, #16970, .T. ) ;
#46150=ORIENTED_EDGE ( 'NONE', *, *, #14587, .T. ) ;
#46152=ADVANCED_FACE ( 'NONE', ( #134615 ), #101239, .T. ) ;
#46154=ORIENTED_EDGE ( 'NONE', *, *, #71240, .F. ) ;
#46156=CARTESIAN_POINT ( 'NONE',  ( -23.99999999999983302, -13.39766691384885000, -10.96608748226460328 ) ) ;
#46159=CARTESIAN_POINT ( 'NONE',  ( 45.29974487139158867, -27.71228299555237840, 4.000000000000000000 ) ) ;
#46162=DIRECTION ( 'NONE',  ( -0.7071067811865487940, 0.7071067811865463515, 0.000000000000000000 ) ) ;
#46163=EDGE_CURVE ( 'NONE', #136547, #74950, #136011, .T. ) ;
#46164=ORIENTED_EDGE ( 'NONE', *, *, #6811, .T. ) ;
#46165=CARTESIAN_POINT ( 'NONE',  ( -0.1839886062690032631, 28.73617430169787568, 5.000000000000000000 ) ) ;
#46167=AXIS2_PLACEMENT_3D ( 'NONE', #87349, #9771, #109074 ) ;
#46168=CARTESIAN_POINT ( 'NONE',  ( -21.70666784232957980, -22.22500000000000142, -0.008920181745145777663 ) ) ;
#46169=ORIENTED_EDGE ( 'NONE', *, *, #37550, .F. ) ;
#46171=LINE ( 'NONE', #79537, #101401 ) ;
#46172=LINE ( 'NONE', #65797, #75244 ) ;
#46173=ADVANCED_FACE ( 'NONE', ( #80940 ), #25824, .T. ) ;
#46174=VERTEX_POINT ( 'NONE', #89652 ) ;
#46176=DIRECTION ( 'NONE',  ( -0.7071067811865486830, -0.7071067811865464625, 0.000000000000000000 ) ) ;
#46178=EDGE_CURVE ( 'NONE', #110261, #64365, #34572, .T. ) ;
#46179=ORIENTED_EDGE ( 'NONE', *, *, #55144, .F. ) ;
#46180=VERTEX_POINT ( 'NONE', #94635 ) ;
#46181=VECTOR ( 'NONE', #120748, 1000.000000000000000 ) ;
#46182=VECTOR ( 'NONE', #33739, 1000.000000000000000 ) ;
#46183=EDGE_CURVE ( 'NONE', #117925, #102633, #26544, .T. ) ;
#46185=VECTOR ( 'NONE', #42108, 999.9999999999998863 ) ;
#46186=LINE ( 'NONE', #13483, #116506 ) ;
#46187=CARTESIAN_POINT ( 'NONE',  ( -5.999999999999954703, -12.03360074219762055, 5.000000000000000000 ) ) ;
#46188=CARTESIAN_POINT ( 'NONE',  ( -15.18398860626900237, 28.73617430169797871, 5.000000000000000000 ) ) ;
#46189=ORIENTED_EDGE ( 'NONE', *, *, #105298, .T. ) ;
#46191=AXIS2_PLACEMENT_3D ( 'NONE', #40308, #128711, #29387 ) ;
#46194=DIRECTION ( 'NONE',  ( -0.000000000000000000, 0.3543493200069153248, 0.9351131265310292928 ) ) ;
#46195=DIRECTION ( 'NONE',  ( -0.7071067811865487940, 0.7071067811865463515, 0.000000000000000000 ) ) ;
#46196=ADVANCED_FACE ( 'NONE', ( #140303 ), #15612, .F. ) ;
#46197=CARTESIAN_POINT ( 'NONE',  ( 34.92499999999998295, 0.8561230773924017878, 4.000000000000000000 ) ) ;
#46199=VERTEX_POINT ( 'NONE', #51886 ) ;
#46201=CARTESIAN_POINT ( 'NONE',  ( -14.99999999999989697, 10.55218569542906337, 5.000000000000000000 ) ) ;
#46202=CARTESIAN_POINT ( 'NONE',  ( -4.823340898400238608, 5.259292476615665457, 15.86257073897099090 ) ) ;
#46204=VECTOR ( 'NONE', #98058, 1000.000000000000000 ) ;
#46206=EDGE_CURVE ( 'NONE', #75908, #54158, #116411, .T. ) ;
#46208=LINE ( 'NONE', #90382, #121854 ) ;
#46209=DIRECTION ( 'NONE',  ( 0.7071067811865487940, -0.7071067811865463515, 0.000000000000000000 ) ) ;
#46210=CARTESIAN_POINT ( 'NONE',  ( -23.99999999999982947, -11.35517001088074629, -1.126524801160163625 ) ) ;
#46211=DIRECTION ( 'NONE',  ( -0.6830127018922180770, -0.6830127018922204085, -0.2588190451025213501 ) ) ;
#46212=CARTESIAN_POINT ( 'NONE',  ( 2.671830600776444076, 11.25929247661560240, 4.000000000000000000 ) ) ;
#46213=CARTESIAN_POINT ( 'NONE',  ( 0.000000000000000000, 0.000000000000000000, 5.000000000000000000 ) ) ;
#46214=ORIENTED_EDGE ( 'NONE', *, *, #79413, .T. ) ;
#46215=ORIENTED_EDGE ( 'NONE', *, *, #11625, .F. ) ;
#46217=DIRECTION ( 'NONE',  ( -0.000000000000000000, 0.3543493200069153248, 0.9351131265310292928 ) ) ;
#46219=CARTESIAN_POINT ( 'NONE',  ( -10.49999999999992184, 8.900465351122141655, -2.516491619111488554 ) ) ;
#46220=ORIENTED_EDGE ( 'NONE', *, *, #57288, .F. ) ;
#46222=ORIENTED_EDGE ( 'NONE', *, *, #58516, .T. ) ;
#46223=LINE ( 'NONE', #46962, #130035 ) ;
#46225=EDGE_LOOP ( 'NONE', ( #69595, #34215, #129658, #107537 ) ) ;
#46226=LINE ( 'NONE', #110007, #107768 ) ;
#46227=EDGE_CURVE ( 'NONE', #111700, #11445, #5475, .T. ) ;
#46230=DIRECTION ( 'NONE',  ( -0.7071067811865487940, 0.7071067811865463515, -0.000000000000000000 ) ) ;
#46231=EDGE_LOOP ( 'NONE', ( #114437, #76832, #47183, #111697 ) ) ;
#46232=LINE ( 'NONE', #89013, #72295 ) ;
#46233=CARTESIAN_POINT ( 'NONE',  ( 21.48921356237309155, -27.52281430457070499, 5.000000000000000000 ) ) ;
#46236=DIRECTION ( 'NONE',  ( -0.7071067811865486830, 0.7071067811865464625, 0.000000000000000000 ) ) ;
#46237=CARTESIAN_POINT ( 'NONE',  ( -45.29974487139158867, -27.71228299555237840, 4.000000000000000000 ) ) ;
#46238=DIRECTION ( 'NONE',  ( -0.000000000000000000, 0.3543493200069153248, 0.9351131265310292928 ) ) ;
#46239=ORIENTED_EDGE ( 'NONE', *, *, #85026, .T. ) ;
#46240=EDGE_CURVE ( 'NONE', #110472, #77537, #117797, .T. ) ;
#46241=CARTESIAN_POINT ( 'NONE',  ( -15.48921356237309510, -27.52281430457066236, 5.000000000000000000 ) ) ;
#46244=CARTESIAN_POINT ( 'NONE',  ( 14.99999999999988809, -5.527737879153178824, -7.983877177622407117 ) ) ;
#46247=DIRECTION ( 'NONE',  ( 0.6830127018922181881, 0.6830127018922202975, -0.2588190451025214056 ) ) ;
#46249=ORIENTED_EDGE ( 'NONE', *, *, #6146, .F. ) ;
#46250=VECTOR ( 'NONE', #105812, 999.9999999999998863 ) ;
#46253=FACE_OUTER_BOUND ( 'NONE', #50302, .T. ) ;
#46254=CARTESIAN_POINT ( 'NONE',  ( -34.92500000000001137, -13.19990548397266394, 4.759050581649336920 ) ) ;
#46255=( BOUNDED_CURVE ( )  B_SPLINE_CURVE ( 3, ( #14622, #56021, #58176, #78464 ),
 .UNSPECIFIED., .F., .T. ) 
 B_SPLINE_CURVE_WITH_KNOTS ( ( 4, 4 ),
 ( 5.106027341939300968, 6.645403452391245303 ),
 .UNSPECIFIED. ) 
 CURVE ( )  GEOMETRIC_REPRESENTATION_ITEM ( )  RATIONAL_B_SPLINE_CURVE ( ( 1.000000000000000000, 0.8120851936182325037, 0.8120851936182325037, 1.000000000000000000 ) ) 
 REPRESENTATION_ITEM ( '' )  );
#46256=VECTOR ( 'NONE', #110620, 1000.000000000000000 ) ;
#46257=CARTESIAN_POINT ( 'NONE',  ( -21.18398860626899349, 28.73617430169802134, 5.000000000000000000 ) ) ;
#46259=LINE ( 'NONE', #80306, #83298 ) ;
#46261=PLANE ( 'NONE',  #109945 ) ;
#46262=VERTEX_POINT ( 'NONE', #72950 ) ;
#46263=PLANE ( 'NONE',  #110787 ) ;
#46264=DIRECTION ( 'NONE',  ( 0.7071067811865487940, 0.7071067811865463515, 0.000000000000000000 ) ) ;
#46265=DIRECTION ( 'NONE',  ( -0.7071067811865486830, 0.7071067811865464625, 0.000000000000000000 ) ) ;
#46266=DIRECTION ( 'NONE',  ( 1.000000000000000000, 0.000000000000000000, 0.000000000000000000 ) ) ;
#46267=VECTOR ( 'NONE', #47835, 1000.000000000000114 ) ;
#46268=DIRECTION ( 'NONE',  ( 0.7071067811865487940, 0.7071067811865463515, -0.000000000000000000 ) ) ;
#46269=ORIENTED_EDGE ( 'NONE', *, *, #36277, .T. ) ;
#46270=ORIENTED_EDGE ( 'NONE', *, *, #125350, .T. ) ;
#46271=ORIENTED_EDGE ( 'NONE', *, *, #5329, .F. ) ;
#46273=AXIS2_PLACEMENT_3D ( 'NONE', #108167, #20461, #64710 ) ;
#46274=ORIENTED_EDGE ( 'NONE', *, *, #134343, .F. ) ;
#46275=PLANE ( 'NONE',  #99524 ) ;
#46276=LINE ( 'NONE', #123822, #78065 ) ;
#46277=VECTOR ( 'NONE', #13894, 1000.000000000000000 ) ;
#46278=VECTOR ( 'NONE', #23997, 999.9999999999998863 ) ;
#46279=CARTESIAN_POINT ( 'NONE',  ( 2.816011393730999401, 28.73617430169785436, 5.000000000000000000 ) ) ;
#46280=CARTESIAN_POINT ( 'NONE',  ( -12.48921356237309155, -27.52281430457064104, 5.000000000000000000 ) ) ;
#46281=EDGE_LOOP ( 'NONE', ( #5608, #109065, #67490, #58886 ) ) ;
#46282=LINE ( 'NONE', #12880, #90780 ) ;
#46283=CARTESIAN_POINT ( 'NONE',  ( -51.18398860626899705, 28.73617430169823095, 5.000000000000000000 ) ) ;
#46284=DIRECTION ( 'NONE',  ( -0.7071067811865486830, -0.7071067811865464625, 0.000000000000000000 ) ) ;
#46287=ORIENTED_EDGE ( 'NONE', *, *, #49325, .F. ) ;
#46288=CARTESIAN_POINT ( 'NONE',  ( -30.70710678118632941, 17.25929247661554200, 5.000000000000000000 ) ) ;
#46289=ADVANCED_FACE ( 'NONE', ( #84514 ), #95360, .F. ) ;
#46290=CARTESIAN_POINT ( 'NONE',  ( 4.499999999999976019, 3.073033219394630144, -6.593910359670959842 ) ) ;
#46291=VECTOR ( 'NONE', #81357, 999.9999999999998863 ) ;
#46292=VECTOR ( 'NONE', #101286, 999.9999999999998863 ) ;
#46293=VERTEX_POINT ( 'NONE', #126549 ) ;
#46294=ORIENTED_EDGE ( 'NONE', *, *, #96324, .T. ) ;
#46295=LINE ( 'NONE', #23041, #116252 ) ;
#46296=EDGE_CURVE ( 'NONE', #26483, #60374, #96063, .T. ) ;
#46300=AXIS2_PLACEMENT_3D ( 'NONE', #95952, #43026, #75650 ) ;
#46301=DIRECTION ( 'NONE',  ( 0.7071067811865486830, -0.7071067811865464625, -0.000000000000000000 ) ) ;
#46302=CARTESIAN_POINT ( 'NONE',  ( 20.51078643762690490, -27.52281430457041012, 5.000000000000000000 ) ) ;
#46303=EDGE_CURVE ( 'NONE', #26872, #114249, #29384, .T. ) ;
#46304=EDGE_CURVE ( 'NONE', #7608, #31464, #117100, .T. ) ;
#46305=DIRECTION ( 'NONE',  ( 0.7071067811865487940, 0.7071067811865463515, 0.000000000000000000 ) ) ;
#46307=VERTEX_POINT ( 'NONE', #138895 ) ;
#46308=ORIENTED_EDGE ( 'NONE', *, *, #54508, .F. ) ;
#46309=CARTESIAN_POINT ( 'NONE',  ( -34.49999999999976552, 6.431123077392124188, 4.000000000000000000 ) ) ;
#46310=EDGE_CURVE ( 'NONE', #130435, #49722, #104070, .T. ) ;
#46311=ORIENTED_EDGE ( 'NONE', *, *, #68444, .T. ) ;
#46312=VERTEX_POINT ( 'NONE', #6886 ) ;
#46313=VECTOR ( 'NONE', #48503, 1000.000000000000000 ) ;
#46314=EDGE_CURVE ( 'NONE', #137089, #34213, #38851, .T. ) ;
#46315=ADVANCED_FACE ( 'NONE', ( #40306 ), #49755, .F. ) ;
#46317=ORIENTED_EDGE ( 'NONE', *, *, #105398, .T. ) ;
#46318=CARTESIAN_POINT ( 'NONE',  ( 29.20666063542132207, 21.75929247661549581, 4.998822639870703632 ) ) ;
#46319=LINE ( 'NONE', #90501, #47288 ) ;
#46320=CARTESIAN_POINT ( 'NONE',  ( 21.18398860626899349, 28.73617430169802134, 5.000000000000000000 ) ) ;
#46321=LINE ( 'NONE', #103486, #39186 ) ;
#46322=VECTOR ( 'NONE', #22731, 1000.000000000000000 ) ;
#46323=DIRECTION ( 'NONE',  ( 1.000000000000000000, 0.000000000000000000, 0.000000000000000000 ) ) ;
#46324=ORIENTED_EDGE ( 'NONE', *, *, #41351, .T. ) ;
#46325=ADVANCED_FACE ( 'NONE', ( #82367 ), #127272, .F. ) ;
#46329=EDGE_LOOP ( 'NONE', ( #78763, #123280, #67829, #108258 ) ) ;
#46330=CARTESIAN_POINT ( 'NONE',  ( -68.99451991528748351, 28.92564299267986172, 4.000000000000000000 ) ) ;
#46332=DIRECTION ( 'NONE',  ( -0.7071067811865486830, -0.7071067811865464625, 0.000000000000000000 ) ) ;
#46333=ORIENTED_EDGE ( 'NONE', *, *, #3423, .T. ) ;
#46335=EDGE_CURVE ( 'NONE', #41303, #79450, #62762, .T. ) ;
#46336=EDGE_LOOP ( 'NONE', ( #113144, #141709, #141025, #52355 ) ) ;
#46337=LINE ( 'NONE', #57206, #111418 ) ;
#46339=CARTESIAN_POINT ( 'NONE',  ( -1.828169399223516400, -17.24070752338410628, 4.000000000000000000 ) ) ;
#46341=CARTESIAN_POINT ( 'NONE',  ( 8.816011393731004731, 28.73617430169781173, 5.000000000000000000 ) ) ;
#46342=CARTESIAN_POINT ( 'NONE',  ( -29.20710678118634362, -8.240707523384196875, 5.000000000000000000 ) ) ;
#46344=EDGE_CURVE ( 'NONE', #104397, #48470, #125875, .T. ) ;
#46345=CARTESIAN_POINT ( 'NONE',  ( -54.18398860626899705, 28.73617430169825226, 5.000000000000000000 ) ) ;
#46346=CARTESIAN_POINT ( 'NONE',  ( -4.499999999999972466, 8.900465351122148761, -2.516491619111501876 ) ) ;
#46351=LINE ( 'NONE', #68803, #15181 ) ;
#46352=DIRECTION ( 'NONE',  ( -0.000000000000000000, 0.000000000000000000, 1.000000000000000000 ) ) ;
#46353=VERTEX_POINT ( 'NONE', #19238 ) ;
#46354=EDGE_CURVE ( 'NONE', #143094, #78582, #20649, .T. ) ;
#46355=ORIENTED_EDGE ( 'NONE', *, *, #80544, .T. ) ;
#46359=ORIENTED_EDGE ( 'NONE', *, *, #90193, .F. ) ;
#46361=EDGE_CURVE ( 'NONE', #34231, #105496, #9017, .T. ) ;
#46362=EDGE_CURVE ( 'NONE', #41654, #19820, #119938, .T. ) ;
#46364=LINE ( 'NONE', #67379, #30628 ) ;
#46365=CARTESIAN_POINT ( 'NONE',  ( 8.816011393731004731, 28.73617430169781173, 5.000000000000000000 ) ) ;
#46366=CARTESIAN_POINT ( 'NONE',  ( -34.92500000000001137, 22.22500000000000142, 4.000000000000000000 ) ) ;
#46367=CARTESIAN_POINT ( 'NONE',  ( -19.27928215921719612, -2.789594763390444321, 4.000000000000000000 ) ) ;
#46368=ORIENTED_EDGE ( 'NONE', *, *, #77243, .F. ) ;
#46370=VECTOR ( 'NONE', #83491, 1000.000000000000000 ) ;
#46371=ORIENTED_EDGE ( 'NONE', *, *, #125635, .F. ) ;
#46372=EDGE_CURVE ( 'NONE', #123433, #138081, #143152, .T. ) ;
#46373=DIRECTION ( 'NONE',  ( 0.7071067811865486830, -0.7071067811865464625, -0.000000000000000000 ) ) ;
#46375=ORIENTED_EDGE ( 'NONE', *, *, #117103, .F. ) ;
#46377=CARTESIAN_POINT ( 'NONE',  ( 36.48921356237310221, -27.52281430457080802, 5.000000000000000000 ) ) ;
#46378=EDGE_CURVE ( 'NONE', #126185, #35333, #140999, .T. ) ;
#46379=CARTESIAN_POINT ( 'NONE',  ( -28.49999999999979750, 7.087461875839173864, 4.000000000000000000 ) ) ;
#46380=VERTEX_POINT ( 'NONE', #32265 ) ;
#46383=DIRECTION ( 'NONE',  ( 0.3543493200069162685, -0.000000000000000000, -0.9351131265310288487 ) ) ;
#46384=VECTOR ( 'NONE', #8500, 1000.000000000000000 ) ;
#46385=LINE ( 'NONE', #79737, #94926 ) ;
#46386=PLANE ( 'NONE',  #999 ) ;
#46387=CARTESIAN_POINT ( 'NONE',  ( -6.792893218813405021, 15.75929247661555976, 5.000000000000000000 ) ) ;
#46388=VERTEX_POINT ( 'NONE', #129414 ) ;
#46389=CARTESIAN_POINT ( 'NONE',  ( 26.99999999999981526, 10.93112307739207267, 4.000000000000000000 ) ) ;
#46390=VECTOR ( 'NONE', #141816, 999.9999999999998863 ) ;
#46394=EDGE_LOOP ( 'NONE', ( #63649, #58260, #138176 ) ) ;
#46395=LINE ( 'NONE', #91986, #93374 ) ;
#46396=VECTOR ( 'NONE', #31246, 1000.000000000000000 ) ;
#46397=EDGE_LOOP ( 'NONE', ( #87787, #120754, #69977, #76981 ) ) ;
#46398=DIRECTION ( 'NONE',  ( -0.7071067811865486830, -0.7071067811865464625, 0.000000000000000000 ) ) ;
#46399=ORIENTED_EDGE ( 'NONE', *, *, #103297, .F. ) ;
#46400=EDGE_CURVE ( 'NONE', #26635, #54672, #43148, .T. ) ;
#46401=ORIENTED_EDGE ( 'NONE', *, *, #104688, .T. ) ;
#46402=AXIS2_PLACEMENT_3D ( 'NONE', #28716, #40318, #72960 ) ;
#46405=EDGE_LOOP ( 'NONE', ( #27483, #16455, #58656, #37289 ) ) ;
#46408=DIRECTION ( 'NONE',  ( -0.7071067811865486830, 0.7071067811865464625, 0.000000000000000000 ) ) ;
#46410=EDGE_CURVE ( 'NONE', #98498, #60519, #64902, .T. ) ;
#46411=FACE_OUTER_BOUND ( 'NONE', #37389, .T. ) ;
#46412=VECTOR ( 'NONE', #83750, 1000.000000000000000 ) ;
#46414=PLANE ( 'NONE',  #9482 ) ;
#46415=DIRECTION ( 'NONE',  ( -0.7071067811865486830, 0.7071067811865464625, 0.000000000000000000 ) ) ;
#46416=CARTESIAN_POINT ( 'NONE',  ( -36.48921356237310221, -27.52281430457080802, 5.000000000000000000 ) ) ;
#46419=AXIS2_PLACEMENT_3D ( 'NONE', #135200, #38710, #46789 ) ;
#46421=DIRECTION ( 'NONE',  ( -0.7071067811865486830, -0.7071067811865464625, -0.000000000000000000 ) ) ;
#46422=FACE_OUTER_BOUND ( 'NONE', #4159, .T. ) ;
#46423=DIRECTION ( 'NONE',  ( -0.7071067811865487940, 0.7071067811865463515, -0.000000000000000000 ) ) ;
#46424=ORIENTED_EDGE ( 'NONE', *, *, #128438, .F. ) ;
#46426=ORIENTED_EDGE ( 'NONE', *, *, #43472, .T. ) ;
#46428=EDGE_CURVE ( 'NONE', #138304, #113129, #75776, .T. ) ;
#46429=ORIENTED_EDGE ( 'NONE', *, *, #66462, .F. ) ;
#46430=ORIENTED_EDGE ( 'NONE', *, *, #125123, .F. ) ;
#46431=ORIENTED_EDGE ( 'NONE', *, *, #88335, .T. ) ;
#46432=CARTESIAN_POINT ( 'NONE',  ( 34.42499999999998295, -6.022814304570537125, 5.000000000000000000 ) ) ;
#46433=PLANE ( 'NONE',  #76471 ) ;
#46434=VECTOR ( 'NONE', #82524, 999.9999999999998863 ) ;
#46436=ORIENTED_EDGE ( 'NONE', *, *, #69032, .F. ) ;
#46437=DIRECTION ( 'NONE',  ( -0.7071067811865486830, -0.7071067811865464625, 0.000000000000000000 ) ) ;
#46438=CARTESIAN_POINT ( 'NONE',  ( 23.99999999999983302, 7.007997736742463957, -8.085015511992057924 ) ) ;
#46439=CARTESIAN_POINT ( 'NONE',  ( -16.92580874392868040, 8.754106587137664874, 4.662926800793050219 ) ) ;
#46440=DIRECTION ( 'NONE',  ( 0.7071067811865487940, -0.7071067811865463515, 0.000000000000000000 ) ) ;
#46441=EDGE_CURVE ( 'NONE', #136084, #110261, #63493, .T. ) ;
#46442=CARTESIAN_POINT ( 'NONE',  ( 20.51078643762690490, -27.52281430457041012, 5.000000000000000000 ) ) ;
#46443=DIRECTION ( 'NONE',  ( -0.3543493200069162685, -0.000000000000000000, -0.9351131265310288487 ) ) ;
#46444=DIRECTION ( 'NONE',  ( -0.7071067811865487940, 0.7071067811865463515, 0.000000000000000000 ) ) ;
#46445=LINE ( 'NONE', #58762, #89205 ) ;
#46446=VECTOR ( 'NONE', #89519, 1000.000000000000000 ) ;
#46447=CARTESIAN_POINT ( 'NONE',  ( 21.61838490601983409, -2.240707523384257716, 13.37739548510234400 ) ) ;
#46448=CARTESIAN_POINT ( 'NONE',  ( 30.48921356237309510, -27.52281430457076894, 5.000000000000000000 ) ) ;
#46452=ORIENTED_EDGE ( 'NONE', *, *, #73533, .T. ) ;
#46453=ORIENTED_EDGE ( 'NONE', *, *, #94565, .T. ) ;
#46456=DIRECTION ( 'NONE',  ( -0.6830127018922181881, 0.6830127018922202975, -0.2588190451025214056 ) ) ;
#46457=VECTOR ( 'NONE', #110272, 1000.000000000000000 ) ;
#46458=CARTESIAN_POINT ( 'NONE',  ( 0.000000000000000000, 0.000000000000000000, 5.000000000000000000 ) ) ;
#46459=DIRECTION ( 'NONE',  ( -0.7071067811865486830, -0.7071067811865464625, 0.000000000000000000 ) ) ;
#46460=VECTOR ( 'NONE', #98517, 1000.000000000000227 ) ;
#46461=AXIS2_PLACEMENT_3D ( 'NONE', #48054, #105269, #93690 ) ;
#46463=EDGE_CURVE ( 'NONE', #74571, #114684, #78159, .T. ) ;
#46464=VERTEX_POINT ( 'NONE', #98237 ) ;
#46466=ORIENTED_EDGE ( 'NONE', *, *, #68927, .F. ) ;
#46468=EDGE_CURVE ( 'NONE', #75609, #124219, #99635, .T. ) ;
#46469=VECTOR ( 'NONE', #138195, 1000.000000000000000 ) ;
#46470=VECTOR ( 'NONE', #136193, 1000.000000000000000 ) ;
#46471=LINE ( 'NONE', #78344, #73266 ) ;
#46472=AXIS2_PLACEMENT_3D ( 'NONE', #78773, #120821, #66475 ) ;
#46473=ORIENTED_EDGE ( 'NONE', *, *, #103877, .T. ) ;
#46475=ORIENTED_EDGE ( 'NONE', *, *, #137310, .F. ) ;
#46476=DIRECTION ( 'NONE',  ( -0.000000000000000000, -0.3543493200069152693, 0.9351131265310292928 ) ) ;
#46477=EDGE_CURVE ( 'NONE', #64566, #57564, #11171, .T. ) ;
#46478=CARTESIAN_POINT ( 'NONE',  ( 33.79289321881321939, -8.240707523384195099, 5.000000000000000000 ) ) ;
#46480=EDGE_CURVE ( 'NONE', #63651, #122408, #40994, .T. ) ;
#46481=EDGE_CURVE ( 'NONE', #100660, #116780, #52571, .T. ) ;
#46483=EDGE_CURVE ( 'NONE', #96125, #35696, #30851, .T. ) ;
#46484=VERTEX_POINT ( 'NONE', #90945 ) ;
#46485=ORIENTED_EDGE ( 'NONE', *, *, #30257, .T. ) ;
#46486=DIRECTION ( 'NONE',  ( 0.7071067811865487940, -0.7071067811865463515, 0.000000000000000000 ) ) ;
#46487=EDGE_CURVE ( 'NONE', #47828, #63098, #69929, .T. ) ;
#46488=ORIENTED_EDGE ( 'NONE', *, *, #9114, .T. ) ;
#46489=EDGE_LOOP ( 'NONE', ( #50905, #78752, #103519, #55474 ) ) ;
#46490=CIRCLE ( 'NONE', #62705, 0.5000000000000000000 ) ;
#46492=EDGE_CURVE ( 'NONE', #83424, #106324, #113367, .T. ) ;
#46493=PLANE ( 'NONE',  #19327 ) ;
#46494=VECTOR ( 'NONE', #55728, 1000.000000000000227 ) ;
#46495=EDGE_CURVE ( 'NONE', #15784, #121472, #46763, .T. ) ;
#46496=AXIS2_PLACEMENT_3D ( 'NONE', #60217, #73233, #49359 ) ;
#46499=ORIENTED_EDGE ( 'NONE', *, *, #41397, .F. ) ;
#46500=DIRECTION ( 'NONE',  ( -0.6830127018922181881, 0.6830127018922202975, -0.2588190451025214056 ) ) ;
#46501=EDGE_CURVE ( 'NONE', #131882, #53582, #101066, .T. ) ;
#46502=AXIS2_PLACEMENT_3D ( 'NONE', #101648, #90052, #92187 ) ;
#46503=FACE_OUTER_BOUND ( 'NONE', #121053, .T. ) ;
#46504=VECTOR ( 'NONE', #129252, 999.9999999999998863 ) ;
#46505=EDGE_CURVE ( 'NONE', #80270, #112794, #79381, .T. ) ;
#46506=FACE_BOUND ( 'NONE', #73482, .T. ) ;
#46507=VERTEX_POINT ( 'NONE', #134442 ) ;
#46508=EDGE_CURVE ( 'NONE', #133473, #97018, #80082, .T. ) ;
#46509=DIRECTION ( 'NONE',  ( -0.000000000000000000, 0.000000000000000000, 1.000000000000000000 ) ) ;
#46510=CARTESIAN_POINT ( 'NONE',  ( 12.29974487139158512, -27.71228299555214747, 4.000000000000000000 ) ) ;
#46511=VECTOR ( 'NONE', #74177, 1000.000000000000000 ) ;
#46513=LINE ( 'NONE', #66088, #50907 ) ;
#46514=ORIENTED_EDGE ( 'NONE', *, *, #88380, .T. ) ;
#46515=DIRECTION ( 'NONE',  ( 0.6830127018922180770, -0.6830127018922204085, -0.2588190451025213501 ) ) ;
#46516=ORIENTED_EDGE ( 'NONE', *, *, #9560, .T. ) ;
#46521=ORIENTED_EDGE ( 'NONE', *, *, #15910, .T. ) ;
#46522=AXIS2_PLACEMENT_3D ( 'NONE', #19786, #64731, #9607 ) ;
#46523=DIRECTION ( 'NONE',  ( -0.7071067811865486830, -0.7071067811865464625, -0.000000000000000000 ) ) ;
#46526=LINE ( 'NONE', #70422, #103787 ) ;
#46527=AXIS2_PLACEMENT_3D ( 'NONE', #70336, #136971, #102923 ) ;
#46528=CARTESIAN_POINT ( 'NONE',  ( -66.29974487139159578, -27.71228299555252406, 4.000000000000000000 ) ) ;
#46530=CARTESIAN_POINT ( 'NONE',  ( 11.99999999999992362, -3.485240976185064010, -4.108735105802371557 ) ) ;
#46531=PLANE ( 'NONE',  #43636 ) ;
#46532=CARTESIAN_POINT ( 'NONE',  ( 1.499999999999996225, 3.052185695429134871, 5.000000000000000000 ) ) ;
#46534=ADVANCED_FACE ( 'NONE', ( #57605 ), #46014, .T. ) ;
#46535=VERTEX_POINT ( 'NONE', #122104 ) ;
#46536=EDGE_LOOP ( 'NONE', ( #57134, #102186, #78199, #56232 ) ) ;
#46537=VECTOR ( 'NONE', #133184, 1000.000000000000227 ) ;
#46538=VERTEX_POINT ( 'NONE', #135856 ) ;
#46539=CARTESIAN_POINT ( 'NONE',  ( -5.700255128608413102, -27.71228299555201957, 4.000000000000000000 ) ) ;
#46540=EDGE_LOOP ( 'NONE', ( #121553, #14847, #62291, #44921 ) ) ;
#46541=EDGE_LOOP ( 'NONE', ( #119703, #95727, #33322, #116391 ) ) ;
#46542=DIRECTION ( 'NONE',  ( -0.6830127018922180770, -0.6830127018922204085, -0.2588190451025213501 ) ) ;
#46543=DIRECTION ( 'NONE',  ( 0.7071067811865486830, -0.7071067811865464625, -0.000000000000000000 ) ) ;
#46544=VERTEX_POINT ( 'NONE', #112668 ) ;
#46545=DIRECTION ( 'NONE',  ( 0.7071067811865487940, 0.7071067811865463515, 0.000000000000000000 ) ) ;
#46546=AXIS2_PLACEMENT_3D ( 'NONE', #84384, #107525, #32115 ) ;
#46547=VECTOR ( 'NONE', #22413, 1000.000000000000227 ) ;
#46549=DIRECTION ( 'NONE',  ( 0.3543493200069163240, 0.000000000000000000, 0.9351131265310288487 ) ) ;
#46551=CARTESIAN_POINT ( 'NONE',  ( 7.499999999999952927, -7.912538124160680475, 4.000000000000000000 ) ) ;
#46554=CARTESIAN_POINT ( 'NONE',  ( 42.29974487139158157, -27.71228299555235708, 4.000000000000000000 ) ) ;
#46555=PLANE ( 'NONE',  #111505 ) ;
#46556=EDGE_CURVE ( 'NONE', #114516, #105099, #124258, .T. ) ;
#46557=CARTESIAN_POINT ( 'NONE',  ( 12.52400138585440459, 22.03583458319438648, 4.979811245910089390 ) ) ;
#46558=ORIENTED_EDGE ( 'NONE', *, *, #92997, .F. ) ;
#46559=FACE_OUTER_BOUND ( 'NONE', #1348, .T. ) ;
#46560=CARTESIAN_POINT ( 'NONE',  ( -17.92867102513379862, 9.037728232668255757, 5.000000000000000000 ) ) ;
#46561=VERTEX_POINT ( 'NONE', #135171 ) ;
#46562=FACE_OUTER_BOUND ( 'NONE', #96310, .T. ) ;
#46563=VERTEX_POINT ( 'NONE', #47468 ) ;
#46564=CARTESIAN_POINT ( 'NONE',  ( -19.93032425809868258, -22.22500000000000142, -0.6820431690203968556 ) ) ;
#46565=VECTOR ( 'NONE', #116019, 1000.000000000000000 ) ;
#46566=LINE ( 'NONE', #124782, #86367 ) ;
#46569=AXIS2_PLACEMENT_3D ( 'NONE', #91073, #57729, #10604 ) ;
#46570=PLANE ( 'NONE',  #113048 ) ;
#46571=EDGE_CURVE ( 'NONE', #134283, #82053, #22761, .T. ) ;
#46572=PLANE ( 'NONE',  #139158 ) ;
#46573=CARTESIAN_POINT ( 'NONE',  ( 5.999999999999958256, -12.03360074219761877, 5.000000000000000000 ) ) ;
#46574=ORIENTED_EDGE ( 'NONE', *, *, #72425, .F. ) ;
#46575=AXIS2_PLACEMENT_3D ( 'NONE', #25639, #125694, #137278 ) ;
#46576=VECTOR ( 'NONE', #40848, 999.9999999999998863 ) ;
#46578=VECTOR ( 'NONE', #12177, 1000.000000000000000 ) ;
#46579=DIRECTION ( 'NONE',  ( -0.7071067811865487940, 0.7071067811865463515, 0.000000000000000000 ) ) ;
#46581=EDGE_LOOP ( 'NONE', ( #70200, #135411, #27574, #46609 ) ) ;
#46582=FACE_OUTER_BOUND ( 'NONE', #102354, .T. ) ;
#46583=DIRECTION ( 'NONE',  ( -0.6830127018922180770, -0.6830127018922204085, -0.2588190451025213501 ) ) ;
#46584=VERTEX_POINT ( 'NONE', #23513 ) ;
#46586=VERTEX_POINT ( 'NONE', #88800 ) ;
#46587=CARTESIAN_POINT ( 'NONE',  ( 14.99999999999989519, 19.93112307739198386, 4.000000000000000000 ) ) ;
#46588=VECTOR ( 'NONE', #143220, 1000.000000000000000 ) ;
#46589=DIRECTION ( 'NONE',  ( -0.000000000000000000, 0.3543493200069153248, 0.9351131265310292928 ) ) ;
#46590=ORIENTED_EDGE ( 'NONE', *, *, #68063, .T. ) ;
#46591=CARTESIAN_POINT ( 'NONE',  ( -16.49999999999987921, -4.912538124160701791, 4.000000000000000000 ) ) ;
#46593=AXIS2_PLACEMENT_3D ( 'NONE', #89410, #46680, #12550 ) ;
#46594=DIRECTION ( 'NONE',  ( -0.7071067811865486830, -0.7071067811865464625, -0.000000000000000000 ) ) ;
#46595=DIRECTION ( 'NONE',  ( -0.7071067811865487940, 0.7071067811865463515, 0.000000000000000000 ) ) ;
#46596=LINE ( 'NONE', #34974, #42416 ) ;
#46597=VECTOR ( 'NONE', #62961, 1000.000000000000000 ) ;
#46598=LINE ( 'NONE', #69760, #102685 ) ;
#46599=LINE ( 'NONE', #111805, #6594 ) ;
#46600=CARTESIAN_POINT ( 'NONE',  ( 31.63753812416075917, 22.22500000000000142, 4.000000000000000000 ) ) ;
#46601=ORIENTED_EDGE ( 'NONE', *, *, #110254, .T. ) ;
#46603=ORIENTED_EDGE ( 'NONE', *, *, #89851, .T. ) ;
#46604=ORIENTED_EDGE ( 'NONE', *, *, #83521, .F. ) ;
#46606=VECTOR ( 'NONE', #100439, 1000.000000000000227 ) ;
#46607=EDGE_CURVE ( 'NONE', #18811, #21087, #67037, .T. ) ;
#46609=ORIENTED_EDGE ( 'NONE', *, *, #16222, .F. ) ;
#46610=VECTOR ( 'NONE', #4142, 1000.000000000000114 ) ;
#46611=ORIENTED_EDGE ( 'NONE', *, *, #47306, .T. ) ;
#46613=CARTESIAN_POINT ( 'NONE',  ( 23.28242261357416254, -21.73023691814493574, 5.000000000000000888 ) ) ;
#46615=ORIENTED_EDGE ( 'NONE', *, *, #37435, .F. ) ;
#46616=CARTESIAN_POINT ( 'NONE',  ( -30.18398860626900060, 28.73617430169808173, 5.000000000000000000 ) ) ;
#46618=DIRECTION ( 'NONE',  ( -0.7071067811865487940, 0.7071067811865463515, -0.000000000000000000 ) ) ;
#46619=CARTESIAN_POINT ( 'NONE',  ( -26.89452376399129818, 22.22500000000000142, 8.043047640789337649 ) ) ;
#46621=VECTOR ( 'NONE', #70486, 1000.000000000000227 ) ;
#46622=ORIENTED_EDGE ( 'NONE', *, *, #24228, .F. ) ;
#46624=DIRECTION ( 'NONE',  ( 0.7071067811865486830, -0.7071067811865464625, -0.000000000000000000 ) ) ;
#46626=FACE_OUTER_BOUND ( 'NONE', #112292, .T. ) ;
#46628=CARTESIAN_POINT ( 'NONE',  ( 1.499999999999991340, -19.91253812416055169, 4.000000000000000000 ) ) ;
#46629=CARTESIAN_POINT ( 'NONE',  ( 3.005480084712505828, 28.92564299267936079, 4.000000000000000000 ) ) ;
#46630=CARTESIAN_POINT ( 'NONE',  ( 12.48921356237309155, -27.52281430457064104, 5.000000000000000000 ) ) ;
#46633=CARTESIAN_POINT ( 'NONE',  ( 17.67183060077634593, -21.74070752338406010, 4.000000000000000000 ) ) ;
#46634=LINE ( 'NONE', #111084, #57759 ) ;
#46636=ORIENTED_EDGE ( 'NONE', *, *, #41495, .F. ) ;
#46637=ORIENTED_EDGE ( 'NONE', *, *, #54130, .T. ) ;
#46639=ORIENTED_EDGE ( 'NONE', *, *, #56028, .F. ) ;
#46640=LINE ( 'NONE', #132908, #124906 ) ;
#46641=ORIENTED_EDGE ( 'NONE', *, *, #92626, .T. ) ;
#46643=DIRECTION ( 'NONE',  ( 0.6830127018922180770, -0.6830127018922204085, -0.2588190451025213501 ) ) ;
#46644=CARTESIAN_POINT ( 'NONE',  ( 0.000000000000000000, 0.000000000000000000, 5.000000000000000000 ) ) ;
#46646=ORIENTED_EDGE ( 'NONE', *, *, #98653, .F. ) ;
#46647=LINE ( 'NONE', #26973, #36320 ) ;
#46648=ORIENTED_EDGE ( 'NONE', *, *, #11572, .F. ) ;
#46649=CIRCLE ( 'NONE', #65138, 5.968999999999998529 ) ;
#46650=CARTESIAN_POINT ( 'NONE',  ( 5.999999999999967137, 14.58746187583909837, 4.000000000000000000 ) ) ;
#46651=DIRECTION ( 'NONE',  ( 0.7071067811865487940, 0.7071067811865463515, 0.000000000000000000 ) ) ;
#46653=FACE_OUTER_BOUND ( 'NONE', #101493, .T. ) ;
#46655=DIRECTION ( 'NONE',  ( -0.3543493200069162685, -0.000000000000000000, -0.9351131265310288487 ) ) ;
#46656=EDGE_LOOP ( 'NONE', ( #143449, #65984, #79151, #77401 ) ) ;
#46657=CARTESIAN_POINT ( 'NONE',  ( -4.214984197241873787, -3.740707523384244837, 15.76143240460122996 ) ) ;
#46658=LINE ( 'NONE', #45214, #80930 ) ;
#46659=CARTESIAN_POINT ( 'NONE',  ( 5.510786437626906675, -27.52281430457051314, 5.000000000000000000 ) ) ;
#46660=VECTOR ( 'NONE', #94865, 1000.000000000000114 ) ;
#46662=EDGE_CURVE ( 'NONE', #124524, #139884, #133723, .T. ) ;
#46665=EDGE_CURVE ( 'NONE', #46724, #55424, #78624, .T. ) ;
#46668=DIRECTION ( 'NONE',  ( 0.7071067811865487940, 0.7071067811865463515, 0.000000000000000000 ) ) ;
#46669=EDGE_CURVE ( 'NONE', #100009, #72242, #16176, .T. ) ;
#46670=CARTESIAN_POINT ( 'NONE',  ( 34.47516574401890921, 7.490517612115553447, 4.998110765256835286 ) ) ;
#46671=EDGE_LOOP ( 'NONE', ( #12197, #49791, #5633, #8462 ) ) ;
#46673=DIRECTION ( 'NONE',  ( 0.7071067811865487940, 0.7071067811865463515, -0.000000000000000000 ) ) ;
#46676=EDGE_CURVE ( 'NONE', #108717, #44302, #84360, .T. ) ;
#46677=( BOUNDED_CURVE ( )  B_SPLINE_CURVE ( 3, ( #104243, #8313, #7615, #140296 ),
 .UNSPECIFIED., .F., .F. ) 
 B_SPLINE_CURVE_WITH_KNOTS ( ( 4, 4 ),
 ( 1.208578181583237710, 1.359146454359485334 ),
 .UNSPECIFIED. ) 
 CURVE ( )  GEOMETRIC_REPRESENTATION_ITEM ( )  RATIONAL_B_SPLINE_CURVE ( ( 1.000000000000000000, 0.9981116584018941973, 0.9981116584018941973, 1.000000000000000000 ) ) 
 REPRESENTATION_ITEM ( '' )  );
#46678=AXIS2_PLACEMENT_3D ( 'NONE', #30810, #75036, #19890 ) ;
#46679=VECTOR ( 'NONE', #77327, 1000.000000000000000 ) ;
#46680=DIRECTION ( 'NONE',  ( 0.6830127018922181881, 0.6830127018922202975, -0.2588190451025214056 ) ) ;
#46682=CARTESIAN_POINT ( 'NONE',  ( 23.99999999999984013, -22.06887692260758982, 4.000000000000000000 ) ) ;
#46683=VECTOR ( 'NONE', #47811, 1000.000000000000000 ) ;
#46684=VECTOR ( 'NONE', #31049, 1000.000000000000000 ) ;
#46685=AXIS2_PLACEMENT_3D ( 'NONE', #100877, #47963, #2982 ) ;
#46686=CARTESIAN_POINT ( 'NONE',  ( -20.99999999999986144, -13.06887692260767686, 4.000000000000000000 ) ) ;
#46687=ADVANCED_FACE ( 'NONE', ( #49593 ), #4553, .F. ) ;
#46688=FACE_BOUND ( 'NONE', #66448, .T. ) ;
#46690=LINE ( 'NONE', #111140, #20198 ) ;
#46693=CARTESIAN_POINT ( 'NONE',  ( 42.48921356237308800, -27.52281430457085065, 5.000000000000000000 ) ) ;
#46694=DIRECTION ( 'NONE',  ( -0.7071067811865487940, 0.7071067811865463515, 0.000000000000000000 ) ) ;
#46695=VERTEX_POINT ( 'NONE', #103209 ) ;
#46697=CARTESIAN_POINT ( 'NONE',  ( -8.700255128608413102, -27.71228299555199825, 4.000000000000000000 ) ) ;
#46698=EDGE_CURVE ( 'NONE', #29986, #29217, #128551, .T. ) ;
#46700=EDGE_LOOP ( 'NONE', ( #19061, #32962, #60187, #56815 ) ) ;
#46702=ORIENTED_EDGE ( 'NONE', *, *, #10968, .F. ) ;
#46703=VECTOR ( 'NONE', #92789, 1000.000000000000227 ) ;
#46704=CARTESIAN_POINT ( 'NONE',  ( 14.99451991528749595, 28.92564299267948513, 4.000000000000000000 ) ) ;
#46705=EDGE_LOOP ( 'NONE', ( #45889, #23730, #8416, #68878 ) ) ;
#46706=DIRECTION ( 'NONE',  ( -0.6830127018922180770, -0.6830127018922204085, -0.2588190451025213501 ) ) ;
#46707=EDGE_CURVE ( 'NONE', #106116, #5533, #27080, .T. ) ;
#46708=AXIS2_PLACEMENT_3D ( 'NONE', #95650, #28276, #18798 ) ;
#46709=LINE ( 'NONE', #134385, #24112 ) ;
#46710=AXIS2_PLACEMENT_3D ( 'NONE', #138980, #139713, #107744 ) ;
#46711=CARTESIAN_POINT ( 'NONE',  ( -4.499999999999962697, -19.91253812416055524, 4.000000000000000000 ) ) ;
#46714=AXIS2_PLACEMENT_3D ( 'NONE', #61843, #27755, #48820 ) ;
#46715=CARTESIAN_POINT ( 'NONE',  ( -20.99999999999985079, 10.55218569542906160, 5.000000000000000000 ) ) ;
#46716=DIRECTION ( 'NONE',  ( -0.7071067811865487940, 0.7071067811865463515, 0.000000000000000000 ) ) ;
#46717=VERTEX_POINT ( 'NONE', #26389 ) ;
#46719=ORIENTED_EDGE ( 'NONE', *, *, #78578, .F. ) ;
#46721=CARTESIAN_POINT ( 'NONE',  ( 25.00051279177633390, 3.647752439586039230, 4.157751055492739489 ) ) ;
#46722=CARTESIAN_POINT ( 'NONE',  ( -12.29974487139158512, -27.71228299555214747, 4.000000000000000000 ) ) ;
#46723=ORIENTED_EDGE ( 'NONE', *, *, #47878, .T. ) ;
#46724=VERTEX_POINT ( 'NONE', #115480 ) ;
#46725=ORIENTED_EDGE ( 'NONE', *, *, #73313, .F. ) ;
#46726=VECTOR ( 'NONE', #107528, 1000.000000000000000 ) ;
#46728=ORIENTED_EDGE ( 'NONE', *, *, #23235, .F. ) ;
#46729=LINE ( 'NONE', #45979, #71764 ) ;
#46734=DIRECTION ( 'NONE',  ( 0.3543493200069162685, -0.000000000000000000, -0.9351131265310288487 ) ) ;
#46736=VECTOR ( 'NONE', #142871, 1000.000000000000000 ) ;
#46737=CARTESIAN_POINT ( 'NONE',  ( -29.29387692260784348, 22.22500000000000142, 4.000000000000000000 ) ) ;
#46738=FACE_OUTER_BOUND ( 'NONE', #44617, .T. ) ;
#46740=AXIS2_PLACEMENT_3D ( 'NONE', #106588, #140668, #119611 ) ;
#46741=ORIENTED_EDGE ( 'NONE', *, *, #112507, .F. ) ;
#46742=DIRECTION ( 'NONE',  ( -0.7071067811865486830, -0.7071067811865464625, 0.000000000000000000 ) ) ;
#46743=CARTESIAN_POINT ( 'NONE',  ( -6.722814304570563948, -21.72499999999999432, 5.000000000000000000 ) ) ;
#46744=LINE ( 'NONE', #90925, #56424 ) ;
#46745=ORIENTED_EDGE ( 'NONE', *, *, #57015, .F. ) ;
#46747=CARTESIAN_POINT ( 'NONE',  ( 57.29974487139158157, -27.71228299555246011, 4.000000000000000000 ) ) ;
#46750=DIRECTION ( 'NONE',  ( -0.7071067811865486830, 0.7071067811865464625, 0.000000000000000000 ) ) ;
#46751=LINE ( 'NONE', #46002, #75054 ) ;
#46752=VECTOR ( 'NONE', #134988, 1000.000000000000000 ) ;
#46753=LINE ( 'NONE', #124250, #124975 ) ;
#46754=DIRECTION ( 'NONE',  ( 0.7071067811865486830, -0.7071067811865464625, -0.000000000000000000 ) ) ;
#46756=FACE_OUTER_BOUND ( 'NONE', #95705, .T. ) ;
#46757=LINE ( 'NONE', #90941, #78467 ) ;
#46758=ORIENTED_EDGE ( 'NONE', *, *, #65072, .F. ) ;
#46759=ADVANCED_FACE ( 'NONE', ( #95188 ), #82220, .T. ) ;
#46761=CIRCLE ( 'NONE', #123089, 5.968999999999998529 ) ;
#46763=LINE ( 'NONE', #2453, #97995 ) ;
#46766=DIRECTION ( 'NONE',  ( -0.7071067811865487940, 0.7071067811865463515, 0.000000000000000000 ) ) ;
#46767=FACE_OUTER_BOUND ( 'NONE', #80415, .T. ) ;
#46769=VERTEX_POINT ( 'NONE', #15454 ) ;
#46772=AXIS2_PLACEMENT_3D ( 'NONE', #97497, #139633, #109092 ) ;
#46775=DIRECTION ( 'NONE',  ( 0.3543493200069162685, -0.000000000000000000, -0.9351131265310288487 ) ) ;
#46777=VECTOR ( 'NONE', #84963, 1000.000000000000000 ) ;
#46778=CARTESIAN_POINT ( 'NONE',  ( 24.79289321881328334, 6.759292476615651246, 5.000000000000000000 ) ) ;
#46779=CARTESIAN_POINT ( 'NONE',  ( 3.722814304570581712, -21.72499999999999432, 5.000000000000000000 ) ) ;
#46780=ADVANCED_FACE ( 'NONE', ( #126391 ), #82916, .F. ) ;
#46781=ORIENTED_EDGE ( 'NONE', *, *, #35715, .F. ) ;
#46783=EDGE_LOOP ( 'NONE', ( #103715, #107681, #23322, #5947 ) ) ;
#46784=AXIS2_PLACEMENT_3D ( 'NONE', #46069, #135903, #91680 ) ;
#46785=DIRECTION ( 'NONE',  ( -0.3543493200069162685, -0.000000000000000000, -0.9351131265310288487 ) ) ;
#46787=PLANE ( 'NONE',  #22926 ) ;
#46789=DIRECTION ( 'NONE',  ( -0.7071067811865486830, -0.7071067811865464625, 0.000000000000000000 ) ) ;
#46790=EDGE_CURVE ( 'NONE', #58576, #115135, #8841, .T. ) ;
#46791=CARTESIAN_POINT ( 'NONE',  ( 5.671830600776434750, 2.259292476615697876, 4.000000000000000000 ) ) ;
#46792=FACE_OUTER_BOUND ( 'NONE', #96666, .T. ) ;
#46793=EDGE_LOOP ( 'NONE', ( #2357, #81649, #133678, #128351, #119251 ) ) ;
#46794=EDGE_CURVE ( 'NONE', #118900, #68320, #19064, .T. ) ;
#46795=VERTEX_POINT ( 'NONE', #129239 ) ;
#46796=DIRECTION ( 'NONE',  ( 0.7071067811865487940, 0.7071067811865463515, 0.000000000000000000 ) ) ;
#46798=VECTOR ( 'NONE', #49492, 1000.000000000000114 ) ;
#46799=LINE ( 'NONE', #90979, #54323 ) ;
#46800=DIRECTION ( 'NONE',  ( -0.7071067811865486830, -0.7071067811865464625, 0.000000000000000000 ) ) ;
#46802=DIRECTION ( 'NONE',  ( -0.7071067811865487940, 0.7071067811865463515, 0.000000000000000000 ) ) ;
#46804=EDGE_LOOP ( 'NONE', ( #133901, #97920, #120947, #41587, #17019 ) ) ;
#46806=DIRECTION ( 'NONE',  ( 0.7071067811865487940, 0.7071067811865463515, 0.000000000000000000 ) ) ;
#46807=CARTESIAN_POINT ( 'NONE',  ( -34.45011844616454511, -1.483719188362514041, 5.000000000000000888 ) ) ;
#46808=CARTESIAN_POINT ( 'NONE',  ( 34.42499999999998295, 22.22500000000000142, 5.000000000000000000 ) ) ;
#46811=VECTOR ( 'NONE', #79510, 1000.000000000000000 ) ;
#46812=CARTESIAN_POINT ( 'NONE',  ( -24.18398860626899705, 28.73617430169804265, 5.000000000000000000 ) ) ;
#46814=DIRECTION ( 'NONE',  ( 0.7071067811865487940, 0.7071067811865463515, 0.000000000000000000 ) ) ;
#46816=AXIS2_PLACEMENT_3D ( 'NONE', #18094, #41305, #106542 ) ;
#46817=LINE ( 'NONE', #80134, #4248 ) ;
#46818=VERTEX_POINT ( 'NONE', #32088 ) ;
#46820=DIRECTION ( 'NONE',  ( -0.000000000000000000, 0.3543493200069153248, 0.9351131265310292928 ) ) ;
#46822=DIRECTION ( 'NONE',  ( -0.7071067811865486830, -0.7071067811865464625, -0.000000000000000000 ) ) ;
#46823=DIRECTION ( 'NONE',  ( -0.7071067811865486830, -0.7071067811865464625, -0.000000000000000000 ) ) ;
#46824=PLANE ( 'NONE',  #128586 ) ;
#46825=VERTEX_POINT ( 'NONE', #95908 ) ;
#46827=CARTESIAN_POINT ( 'NONE',  ( 36.18398860626899705, 28.73617430169812437, 5.000000000000000000 ) ) ;
#46828=DIRECTION ( 'NONE',  ( -0.7071067811865487940, 0.7071067811865463515, -0.000000000000000000 ) ) ;
#46830=VERTEX_POINT ( 'NONE', #53865 ) ;
#46833=ADVANCED_FACE ( 'NONE', ( #142295 ), #76315, .F. ) ;
#46834=ORIENTED_EDGE ( 'NONE', *, *, #129554, .F. ) ;
#46835=FACE_OUTER_BOUND ( 'NONE', #136191, .T. ) ;
#46836=EDGE_CURVE ( 'NONE', #16024, #37562, #129976, .T. ) ;
#46837=DIRECTION ( 'NONE',  ( 0.6830127018922180770, -0.6830127018922204085, -0.2588190451025213501 ) ) ;
#46838=FACE_OUTER_BOUND ( 'NONE', #125860, .T. ) ;
#46839=AXIS2_PLACEMENT_3D ( 'NONE', #118625, #129494, #38936 ) ;
#46840=DIRECTION ( 'NONE',  ( -0.000000000000000000, 0.000000000000000000, 1.000000000000000000 ) ) ;
#46842=EDGE_LOOP ( 'NONE', ( #35606, #33552, #124355, #43609 ) ) ;
#46843=ORIENTED_EDGE ( 'NONE', *, *, #132405, .T. ) ;
#46844=AXIS2_PLACEMENT_3D ( 'NONE', #61562, #82569, #39060 ) ;
#46845=LINE ( 'NONE', #112056, #63058 ) ;
#46847=EDGE_CURVE ( 'NONE', #86268, #76404, #140824, .T. ) ;
#46848=EDGE_CURVE ( 'NONE', #94406, #119070, #30679, .T. ) ;
#46849=ORIENTED_EDGE ( 'NONE', *, *, #80188, .T. ) ;
#46850=FACE_OUTER_BOUND ( 'NONE', #74833, .T. ) ;
#46852=CARTESIAN_POINT ( 'NONE',  ( -4.499999999999966249, -11.56887692260769462, 4.000000000000000000 ) ) ;
#46853=VECTOR ( 'NONE', #88615, 1000.000000000000000 ) ;
#46855=EDGE_CURVE ( 'NONE', #68379, #65716, #98062, .T. ) ;
#46856=FACE_BOUND ( 'NONE', #49445, .T. ) ;
#46857=EDGE_CURVE ( 'NONE', #123709, #77093, #119774, .T. ) ;
#46858=DIRECTION ( 'NONE',  ( 0.7071067811865487940, 0.7071067811865463515, -0.000000000000000000 ) ) ;
#46859=CARTESIAN_POINT ( 'NONE',  ( -15.18398860626900237, 28.73617430169797871, 5.000000000000000000 ) ) ;
#46860=DIRECTION ( 'NONE',  ( 0.6830127018922180770, -0.6830127018922204085, -0.2588190451025213501 ) ) ;
#46861=AXIS2_PLACEMENT_3D ( 'NONE', #135384, #36745, #101292 ) ;
#46863=( BOUNDED_CURVE ( )  B_SPLINE_CURVE ( 3, ( #45877, #12494, #132893, #100238 ),
 .UNSPECIFIED., .F., .T. ) 
 B_SPLINE_CURVE_WITH_KNOTS ( ( 4, 4 ),
 ( 5.106027341939290309, 6.645403452391244414 ),
 .UNSPECIFIED. ) 
 CURVE ( )  GEOMETRIC_REPRESENTATION_ITEM ( )  RATIONAL_B_SPLINE_CURVE ( ( 1.000000000000000000, 0.8120851936182302833, 0.8120851936182302833, 1.000000000000000000 ) ) 
 REPRESENTATION_ITEM ( '' )  );
#46866=EDGE_LOOP ( 'NONE', ( #50322, #107062, #113334, #52438 ) ) ;
#46867=VERTEX_POINT ( 'NONE', #121220 ) ;
#46869=VERTEX_POINT ( 'NONE', #87891 ) ;
#46870=EDGE_CURVE ( 'NONE', #66621, #50596, #85739, .T. ) ;
#46871=LINE ( 'NONE', #12735, #62814 ) ;
#46872=ORIENTED_EDGE ( 'NONE', *, *, #90169, .T. ) ;
#46873=FACE_OUTER_BOUND ( 'NONE', #122608, .T. ) ;
#46876=VECTOR ( 'NONE', #91286, 1000.000000000000114 ) ;
#46878=LINE ( 'NONE', #3289, #64027 ) ;
#46880=DIRECTION ( 'NONE',  ( -0.000000000000000000, -0.3543493200069152693, 0.9351131265310292928 ) ) ;
#46881=EDGE_LOOP ( 'NONE', ( #51799, #25487, #109725, #124967 ) ) ;
#46884=LINE ( 'NONE', #125089, #119846 ) ;
#46885=CARTESIAN_POINT ( 'NONE',  ( -32.95341186370436048, 14.25929247661557042, 18.84478104361335227 ) ) ;
#46886=DIRECTION ( 'NONE',  ( 0.7071067811865487940, -0.7071067811865463515, 0.000000000000000000 ) ) ;
#46888=VECTOR ( 'NONE', #69071, 1000.000000000000000 ) ;
#46889=EDGE_CURVE ( 'NONE', #25969, #63809, #106772, .T. ) ;
#46891=AXIS2_PLACEMENT_3D ( 'NONE', #43070, #143071, #97394 ) ;
#46892=LINE ( 'NONE', #12748, #65307 ) ;
#46893=VERTEX_POINT ( 'NONE', #64008 ) ;
#46895=CARTESIAN_POINT ( 'NONE',  ( -20.99999999999984368, -19.44781430457063465, 5.000000000000000000 ) ) ;
#46896=ORIENTED_EDGE ( 'NONE', *, *, #124158, .F. ) ;
#46897=VERTEX_POINT ( 'NONE', #75602 ) ;
#46898=VERTEX_POINT ( 'NONE', #97303 ) ;
#46902=ORIENTED_EDGE ( 'NONE', *, *, #76032, .T. ) ;
#46903=EDGE_CURVE ( 'NONE', #89022, #68720, #140151, .T. ) ;
#46906=LINE ( 'NONE', #78769, #44894 ) ;
#46907=ORIENTED_EDGE ( 'NONE', *, *, #63569, .T. ) ;
#46909=PLANE ( 'NONE',  #82700 ) ;
#46910=ORIENTED_EDGE ( 'NONE', *, *, #90825, .T. ) ;
#46911=DIRECTION ( 'NONE',  ( 0.6830127018922180770, -0.6830127018922204085, -0.2588190451025213501 ) ) ;
#46912=VERTEX_POINT ( 'NONE', #24770 ) ;
#46913=CARTESIAN_POINT ( 'NONE',  ( -12.18398860626900060, 28.73617430169795739, 5.000000000000000000 ) ) ;
#46915=DIRECTION ( 'NONE',  ( -0.7071067811865487940, 0.7071067811865463515, 0.000000000000000000 ) ) ;
#46917=VERTEX_POINT ( 'NONE', #133550 ) ;
#46918=FACE_OUTER_BOUND ( 'NONE', #45998, .T. ) ;
#46919=ORIENTED_EDGE ( 'NONE', *, *, #69792, .T. ) ;
#46920=VECTOR ( 'NONE', #84660, 1000.000000000000000 ) ;
#46921=ORIENTED_EDGE ( 'NONE', *, *, #2039, .F. ) ;
#46922=ORIENTED_EDGE ( 'NONE', *, *, #71691, .F. ) ;
#46924=DIRECTION ( 'NONE',  ( -0.000000000000000000, 0.000000000000000000, 1.000000000000000000 ) ) ;
#46925=DIRECTION ( 'NONE',  ( -0.000000000000000000, 0.3543493200069153248, 0.9351131265310292928 ) ) ;
#46926=PLANE ( 'NONE',  #18724 ) ;
#46927=ORIENTED_EDGE ( 'NONE', *, *, #117739, .T. ) ;
#46929=DIRECTION ( 'NONE',  ( -0.3543493200069162685, -0.000000000000000000, -0.9351131265310288487 ) ) ;
#46930=LINE ( 'NONE', #35315, #78407 ) ;
#46931=DIRECTION ( 'NONE',  ( 0.6830127018922180770, -0.6830127018922204085, -0.2588190451025213501 ) ) ;
#46932=EDGE_LOOP ( 'NONE', ( #47696, #21192, #38656 ) ) ;
#46933=VERTEX_POINT ( 'NONE', #118363 ) ;
#46935=VECTOR ( 'NONE', #41794, 1000.000000000000227 ) ;
#46936=ORIENTED_EDGE ( 'NONE', *, *, #123013, .T. ) ;
#46937=FACE_OUTER_BOUND ( 'NONE', #62010, .T. ) ;
#46939=FACE_OUTER_BOUND ( 'NONE', #83269, .T. ) ;
#46940=DIRECTION ( 'NONE',  ( -0.6830127018922180770, -0.6830127018922204085, -0.2588190451025213501 ) ) ;
#46942=CARTESIAN_POINT ( 'NONE',  ( -60.18398860626900415, 28.73617430169829490, 5.000000000000000000 ) ) ;
#46943=DIRECTION ( 'NONE',  ( 0.7071067811865486830, -0.7071067811865464625, -0.000000000000000000 ) ) ;
#46946=CARTESIAN_POINT ( 'NONE',  ( -7.499999999999947597, 15.43112307739203182, 4.000000000000000000 ) ) ;
#46947=VERTEX_POINT ( 'NONE', #44423 ) ;
#46948=AXIS2_PLACEMENT_3D ( 'NONE', #44500, #66935, #45216 ) ;
#46950=VERTEX_POINT ( 'NONE', #91473 ) ;
#46952=LINE ( 'NONE', #48326, #71910 ) ;
#46956=CARTESIAN_POINT ( 'NONE',  ( -23.99999999999983658, -13.44781430457069149, 5.000000000000000000 ) ) ;
#46957=ORIENTED_EDGE ( 'NONE', *, *, #32683, .F. ) ;
#46958=EDGE_CURVE ( 'NONE', #51427, #7365, #90019, .T. ) ;
#46959=CARTESIAN_POINT ( 'NONE',  ( -0.4892135623730947680, -27.52281430457055578, 5.000000000000000000 ) ) ;
#46960=VECTOR ( 'NONE', #69612, 1000.000000000000000 ) ;
#46961=ORIENTED_EDGE ( 'NONE', *, *, #18551, .F. ) ;
#46962=CARTESIAN_POINT ( 'NONE',  ( 21.29974487139158512, -27.71228299555221142, 4.000000000000000000 ) ) ;
#46963=ORIENTED_EDGE ( 'NONE', *, *, #130439, .T. ) ;
#46964=EDGE_CURVE ( 'NONE', #43938, #46917, #13158, .T. ) ;
#46965=CARTESIAN_POINT ( 'NONE',  ( 6.717577386425625185, -21.73023691814492508, 5.000000000000001776 ) ) ;
#46967=FACE_OUTER_BOUND ( 'NONE', #97403, .T. ) ;
#46968=DIRECTION ( 'NONE',  ( 0.7071067811865487940, 0.7071067811865463515, 0.000000000000000000 ) ) ;
#46969=ORIENTED_EDGE ( 'NONE', *, *, #6187, .F. ) ;
#46970=ADVANCED_FACE ( 'NONE', ( #13868 ), #121921, .F. ) ;
#46971=CARTESIAN_POINT ( 'NONE',  ( 75.18398860626899705, 28.73617430169839793, 5.000000000000000000 ) ) ;
#46973=CARTESIAN_POINT ( 'NONE',  ( -57.18398860626899705, 28.73617430169827358, 5.000000000000000000 ) ) ;
#46976=AXIS2_PLACEMENT_3D ( 'NONE', #126228, #25463, #34956 ) ;
#46977=VECTOR ( 'NONE', #133979, 1000.000000000000000 ) ;
#46979=LINE ( 'NONE', #112884, #138145 ) ;
#46980=VERTEX_POINT ( 'NONE', #34233 ) ;
#46981=VECTOR ( 'NONE', #37799, 1000.000000000000000 ) ;
#46982=EDGE_CURVE ( 'NONE', #14592, #78770, #112500, .T. ) ;
#46983=VECTOR ( 'NONE', #141695, 1000.000000000000000 ) ;
#46984=CARTESIAN_POINT ( 'NONE',  ( -19.05000000000000071, 3.174999999999997158, 5.000000000000000000 ) ) ;
#46985=VERTEX_POINT ( 'NONE', #36376 ) ;
#46987=CARTESIAN_POINT ( 'NONE',  ( -34.42500000000001137, -21.72500000000000142, 5.000000000000000000 ) ) ;
#46988=DIRECTION ( 'NONE',  ( 0.3543493200069163240, -0.000000000000000000, -0.9351131265310288487 ) ) ;
#46989=VECTOR ( 'NONE', #52446, 1000.000000000000000 ) ;
#46990=VECTOR ( 'NONE', #112892, 1000.000000000000227 ) ;
#46991=CARTESIAN_POINT ( 'NONE',  ( 11.99999999999991651, 1.552185695429147527, 5.000000000000000000 ) ) ;
#46993=ORIENTED_EDGE ( 'NONE', *, *, #28515, .T. ) ;
#46994=EDGE_CURVE ( 'NONE', #9906, #48450, #11728, .T. ) ;
#46995=DIRECTION ( 'NONE',  ( -0.6830127018922181881, 0.6830127018922202975, -0.2588190451025214056 ) ) ;
#46996=DIRECTION ( 'NONE',  ( 0.7071067811865487940, 0.7071067811865463515, 0.000000000000000000 ) ) ;
#46999=CARTESIAN_POINT ( 'NONE',  ( -45.29974487139158867, -27.71228299555237840, 4.000000000000000000 ) ) ;
#47000=DIRECTION ( 'NONE',  ( 1.000000000000000000, 0.000000000000000000, 0.000000000000000000 ) ) ;
#47003=EDGE_CURVE ( 'NONE', #68079, #28957, #45843, .T. ) ;
#47005=PLANE ( 'NONE',  #118706 ) ;
#47006=DIRECTION ( 'NONE',  ( 0.7071067811865487940, 0.7071067811865463515, 0.000000000000000000 ) ) ;
#47007=PLANE ( 'NONE',  #84046 ) ;
#47008=ORIENTED_EDGE ( 'NONE', *, *, #132094, .T. ) ;
#47009=VERTEX_POINT ( 'NONE', #56012 ) ;
#47010=VERTEX_POINT ( 'NONE', #854 ) ;
#47012=ORIENTED_EDGE ( 'NONE', *, *, #34832, .F. ) ;
#47013=DIRECTION ( 'NONE',  ( 0.6830127018922180770, -0.6830127018922204085, -0.2588190451025213501 ) ) ;
#47014=EDGE_CURVE ( 'NONE', #78177, #4434, #55277, .T. ) ;
#47017=CARTESIAN_POINT ( 'NONE',  ( 5.999999999999956479, 9.631307414974335401, -9.079085613539529476 ) ) ;
#47018=ORIENTED_EDGE ( 'NONE', *, *, #82658, .T. ) ;
#47019=CARTESIAN_POINT ( 'NONE',  ( 22.94836012241460566, 22.22500000000000142, 26.93037957019046758 ) ) ;
#47020=CARTESIAN_POINT ( 'NONE',  ( 18.18398860626898994, 28.73617430169800002, 5.000000000000000000 ) ) ;
#47021=VECTOR ( 'NONE', #97829, 1000.000000000000000 ) ;
#47022=EDGE_CURVE ( 'NONE', #51777, #60758, #89321, .T. ) ;
#47023=EDGE_CURVE ( 'NONE', #62799, #99425, #1554, .T. ) ;
#47024=CARTESIAN_POINT ( 'NONE',  ( 17.99999999999987566, -13.97847968911258754, -0.1324546996126375054 ) ) ;
#47026=ORIENTED_EDGE ( 'NONE', *, *, #8217, .F. ) ;
#47027=VECTOR ( 'NONE', #73455, 1000.000000000000000 ) ;
#47028=CARTESIAN_POINT ( 'NONE',  ( -20.27718569542926730, -21.72500000000000853, 5.000000000000000000 ) ) ;
#47029=DIRECTION ( 'NONE',  ( 0.7071067811865486830, -0.7071067811865464625, -0.000000000000000000 ) ) ;
#47030=AXIS2_PLACEMENT_3D ( 'NONE', #39473, #27856, #104703 ) ;
#47032=EDGE_CURVE ( 'NONE', #51730, #116759, #79202, .T. ) ;
#47033=VERTEX_POINT ( 'NONE', #2268 ) ;
#47034=EDGE_LOOP ( 'NONE', ( #44098, #57386, #111419, #56288 ) ) ;
#47035=CARTESIAN_POINT ( 'NONE',  ( -15.18398860626900237, 28.73617430169797871, 5.000000000000000000 ) ) ;
#47036=EDGE_CURVE ( 'NONE', #903, #16634, #90773, .T. ) ;
#47037=ADVANCED_FACE ( 'NONE', ( #61713 ), #114621, .T. ) ;
#47041=DIRECTION ( 'NONE',  ( -0.6830127018922180770, -0.6830127018922204085, -0.2588190451025213501 ) ) ;
#47042=CARTESIAN_POINT ( 'NONE',  ( -11.20710678118646086, -17.24070752338409918, 5.000000000000000000 ) ) ;
#47043=VECTOR ( 'NONE', #86311, 1000.000000000000000 ) ;
#47046=ORIENTED_EDGE ( 'NONE', *, *, #29957, .T. ) ;
#47047=ORIENTED_EDGE ( 'NONE', *, *, #101716, .F. ) ;
#47048=EDGE_CURVE ( 'NONE', #51626, #97582, #103732, .T. ) ;
#47050=ORIENTED_EDGE ( 'NONE', *, *, #47036, .T. ) ;
#47051=EDGE_LOOP ( 'NONE', ( #137249, #125521, #121416, #42710 ) ) ;
#47052=VECTOR ( 'NONE', #24344, 1000.000000000000000 ) ;
#47053=AXIS2_PLACEMENT_3D ( 'NONE', #69229, #14097, #37301 ) ;
#47054=EDGE_CURVE ( 'NONE', #70774, #114684, #103940, .T. ) ;
#47056=ORIENTED_EDGE ( 'NONE', *, *, #34695, .T. ) ;
#47057=DIRECTION ( 'NONE',  ( 0.7071067811865487940, 0.7071067811865463515, -0.000000000000000000 ) ) ;
#47058=CARTESIAN_POINT ( 'NONE',  ( -26.67183060077628554, -0.7407075233842701500, 4.000000000000000000 ) ) ;
#47059=CARTESIAN_POINT ( 'NONE',  ( 4.499999999999968914, 13.46639925780212366, 5.000000000000000000 ) ) ;
#47060=CARTESIAN_POINT ( 'NONE',  ( -0.6431874275173860012, -20.24070752338407786, 21.22881796311212810 ) ) ;
#47061=VECTOR ( 'NONE', #63588, 1000.000000000000000 ) ;
#47062=DIRECTION ( 'NONE',  ( -0.000000000000000000, -0.3543493200069152693, 0.9351131265310292928 ) ) ;
#47063=ORIENTED_EDGE ( 'NONE', *, *, #84917, .T. ) ;
#47065=ORIENTED_EDGE ( 'NONE', *, *, #46903, .F. ) ;
#47067=ORIENTED_EDGE ( 'NONE', *, *, #97328, .T. ) ;
#47068=DIRECTION ( 'NONE',  ( -0.7071067811865487940, 0.7071067811865463515, -0.000000000000000000 ) ) ;
#47069=ORIENTED_EDGE ( 'NONE', *, *, #46848, .F. ) ;
#47070=LINE ( 'NONE', #15740, #87521 ) ;
#47072=ORIENTED_EDGE ( 'NONE', *, *, #87704, .T. ) ;
#47073=VECTOR ( 'NONE', #25174, 1000.000000000000227 ) ;
#47074=ORIENTED_EDGE ( 'NONE', *, *, #8789, .T. ) ;
#47077=ADVANCED_FACE ( 'NONE', ( #103053 ), #59573, .F. ) ;
#47081=DIRECTION ( 'NONE',  ( -0.000000000000000000, -0.3543493200069152693, 0.9351131265310292928 ) ) ;
#47082=EDGE_CURVE ( 'NONE', #63122, #9882, #92881, .T. ) ;
#47083=DIRECTION ( 'NONE',  ( -0.7071067811865487940, 0.7071067811865463515, 0.000000000000000000 ) ) ;
#47086=DIRECTION ( 'NONE',  ( -0.6830127018922180770, -0.6830127018922204085, -0.2588190451025213501 ) ) ;
#47087=VECTOR ( 'NONE', #114573, 1000.000000000000000 ) ;
#47088=DIRECTION ( 'NONE',  ( -0.7071067811865486830, -0.7071067811865464625, 0.000000000000000000 ) ) ;
#47089=EDGE_LOOP ( 'NONE', ( #35034, #46514, #110461, #30525 ) ) ;
#47090=DIRECTION ( 'NONE',  ( 0.7071067811865486830, -0.7071067811865464625, -0.000000000000000000 ) ) ;
#47092=VERTEX_POINT ( 'NONE', #4376 ) ;
#47093=AXIS2_PLACEMENT_3D ( 'NONE', #65360, #109542, #53760 ) ;
#47095=ORIENTED_EDGE ( 'NONE', *, *, #89679, .T. ) ;
#47096=CARTESIAN_POINT ( 'NONE',  ( 0.000000000000000000, 0.000000000000000000, 5.000000000000000000 ) ) ;
#47097=CARTESIAN_POINT ( 'NONE',  ( 11.99999999999992362, 17.96639925780207747, 5.000000000000000000 ) ) ;
#47098=LINE ( 'NONE', #135490, #85720 ) ;
#47099=CARTESIAN_POINT ( 'NONE',  ( -42.18398860626899705, 28.73617430169816700, 5.000000000000000000 ) ) ;
#47100=ORIENTED_EDGE ( 'NONE', *, *, #81387, .F. ) ;
#47101=DIRECTION ( 'NONE',  ( 0.7071067811865486830, -0.7071067811865464625, -0.000000000000000000 ) ) ;
#47103=CARTESIAN_POINT ( 'NONE',  ( 66.29974487139159578, -27.71228299555252406, 4.000000000000000000 ) ) ;
#47104=VECTOR ( 'NONE', #32097, 1000.000000000000000 ) ;
#47106=ORIENTED_EDGE ( 'NONE', *, *, #30946, .T. ) ;
#47108=DIRECTION ( 'NONE',  ( -0.6830127018922181881, 0.6830127018922202975, -0.2588190451025214056 ) ) ;
#47109=VERTEX_POINT ( 'NONE', #15287 ) ;
#47110=ORIENTED_EDGE ( 'NONE', *, *, #57932, .F. ) ;
#47111=EDGE_LOOP ( 'NONE', ( #123933, #78360, #67071, #33783 ) ) ;
#47112=DIRECTION ( 'NONE',  ( -0.000000000000000000, 0.000000000000000000, 1.000000000000000000 ) ) ;
#47113=FACE_OUTER_BOUND ( 'NONE', #22283, .T. ) ;
#47114=LINE ( 'NONE', #92674, #137638 ) ;
#47115=DIRECTION ( 'NONE',  ( -0.000000000000000000, 0.3543493200069153248, 0.9351131265310292928 ) ) ;
#47116=ORIENTED_EDGE ( 'NONE', *, *, #48538, .T. ) ;
#47117=AXIS2_PLACEMENT_3D ( 'NONE', #106187, #104047, #127247 ) ;
#47118=PLANE ( 'NONE',  #87932 ) ;
#47120=VECTOR ( 'NONE', #19915, 1000.000000000000227 ) ;
#47121=CARTESIAN_POINT ( 'NONE',  ( -21.29974487139158512, -27.71228299555221142, 4.000000000000000000 ) ) ;
#47122=PLANE ( 'NONE',  #58441 ) ;
#47123=EDGE_LOOP ( 'NONE', ( #96243, #3156, #2590, #79657 ) ) ;
#47124=CARTESIAN_POINT ( 'NONE',  ( 21.18398860626899349, 28.73617430169802134, 5.000000000000000000 ) ) ;
#47125=VERTEX_POINT ( 'NONE', #48677 ) ;
#47127=AXIS2_PLACEMENT_3D ( 'NONE', #10474, #120660, #21379 ) ;
#47130=EDGE_LOOP ( 'NONE', ( #8076, #134449, #112481, #26093 ) ) ;
#47131=VERTEX_POINT ( 'NONE', #5123 ) ;
#47132=EDGE_CURVE ( 'NONE', #14903, #44540, #95002, .T. ) ;
#47133=ADVANCED_FACE ( 'NONE', ( #37819 ), #58895, .F. ) ;
#47134=CARTESIAN_POINT ( 'NONE',  ( -21.18398860626899349, 28.73617430169802134, 5.000000000000000000 ) ) ;
#47136=ORIENTED_EDGE ( 'NONE', *, *, #53166, .F. ) ;
#47138=ORIENTED_EDGE ( 'NONE', *, *, #44508, .T. ) ;
#47139=VECTOR ( 'NONE', #5422, 1000.000000000000000 ) ;
#47141=ADVANCED_FACE ( 'NONE', ( #29752 ), #87006, .T. ) ;
#47142=CARTESIAN_POINT ( 'NONE',  ( -13.49999999999990408, -1.912538124160735542, 4.000000000000000000 ) ) ;
#47143=DIRECTION ( 'NONE',  ( -0.7071067811865487940, 0.7071067811865463515, -0.000000000000000000 ) ) ;
#47144=LINE ( 'NONE', #79763, #39316 ) ;
#47145=VECTOR ( 'NONE', #83043, 1000.000000000000000 ) ;
#47146=DIRECTION ( 'NONE',  ( -2.781805975412905890E-17, 0.3543493200069152693, 0.9351131265310292928 ) ) ;
#47147=DIRECTION ( 'NONE',  ( 0.000000000000000000, 0.000000000000000000, 1.000000000000000000 ) ) ;
#47149=CARTESIAN_POINT ( 'NONE',  ( 33.18398860626899705, 28.73617430169810305, 5.000000000000000000 ) ) ;
#47150=DIRECTION ( 'NONE',  ( -0.7071067811865486830, -0.7071067811865464625, -0.000000000000000000 ) ) ;
#47153=CARTESIAN_POINT ( 'NONE',  ( -31.43312800248722994, -21.74070752338405654, 6.915939825044148392 ) ) ;
#47156=DIRECTION ( 'NONE',  ( -0.000000000000000000, 0.000000000000000000, 1.000000000000000000 ) ) ;
#47157=EDGE_LOOP ( 'NONE', ( #50954, #134592, #2905 ) ) ;
#47160=EDGE_CURVE ( 'NONE', #119701, #92286, #129073, .T. ) ;
#47163=ORIENTED_EDGE ( 'NONE', *, *, #4673, .T. ) ;
#47164=CARTESIAN_POINT ( 'NONE',  ( 9.183988606268997046, 28.73617430169793607, 5.000000000000000000 ) ) ;
#47165=PLANE ( 'NONE',  #106414 ) ;
#47168=EDGE_LOOP ( 'NONE', ( #77137, #27634, #26918 ) ) ;
#47169=LINE ( 'NONE', #79786, #11544 ) ;
#47170=LINE ( 'NONE', #91350, #58106 ) ;
#47171=DIRECTION ( 'NONE',  ( -0.000000000000000000, 0.000000000000000000, 1.000000000000000000 ) ) ;
#47172=CARTESIAN_POINT ( 'NONE',  ( 29.99999999999979750, -3.033600742197707145, 5.000000000000000000 ) ) ;
#47173=CARTESIAN_POINT ( 'NONE',  ( 56.99451991528749062, 28.92564299267978001, 4.000000000000000000 ) ) ;
#47174=CARTESIAN_POINT ( 'NONE',  ( 0.000000000000000000, 0.000000000000000000, 5.000000000000000000 ) ) ;
#47175=CARTESIAN_POINT ( 'NONE',  ( -1.499999999999990896, -17.56887692260763956, 4.000000000000000000 ) ) ;
#47176=VECTOR ( 'NONE', #125777, 1000.000000000000000 ) ;
#47177=EDGE_CURVE ( 'NONE', #39146, #3561, #20298, .T. ) ;
#47179=CARTESIAN_POINT ( 'NONE',  ( 27.79289321881326558, -17.24070752338409918, 5.000000000000000000 ) ) ;
#47181=LINE ( 'NONE', #136984, #60773 ) ;
#47182=ORIENTED_EDGE ( 'NONE', *, *, #85559, .T. ) ;
#47183=ORIENTED_EDGE ( 'NONE', *, *, #112541, .F. ) ;
#47186=ORIENTED_EDGE ( 'NONE', *, *, #116771, .F. ) ;
#47187=ADVANCED_FACE ( 'NONE', ( #9401 ), #73998, .T. ) ;
#47188=CARTESIAN_POINT ( 'NONE',  ( 33.09667064187385677, -2.240707523384257716, 15.26439735382760077 ) ) ;
#47189=DIRECTION ( 'NONE',  ( -0.3543493200069162685, -0.000000000000000000, -0.9351131265310288487 ) ) ;
#47190=FACE_OUTER_BOUND ( 'NONE', #70795, .T. ) ;
#47191=DIRECTION ( 'NONE',  ( 0.6830127018922180770, -0.6830127018922204085, -0.2588190451025213501 ) ) ;
#47192=VECTOR ( 'NONE', #34699, 1000.000000000000000 ) ;
#47193=EDGE_CURVE ( 'NONE', #54301, #104648, #53689, .T. ) ;
#47195=VERTEX_POINT ( 'NONE', #31916 ) ;
#47196=EDGE_CURVE ( 'NONE', #70864, #26964, #31213, .T. ) ;
#47197=ORIENTED_EDGE ( 'NONE', *, *, #95412, .F. ) ;
#47198=DIRECTION ( 'NONE',  ( -0.000000000000000000, -0.3543493200069152693, 0.9351131265310292928 ) ) ;
#47200=CARTESIAN_POINT ( 'NONE',  ( -13.82816939922343913, -2.240707523384255939, 4.000000000000000000 ) ) ;
#47201=ADVANCED_FACE ( 'NONE', ( #54412 ), #95738, .F. ) ;
#47202=ORIENTED_EDGE ( 'NONE', *, *, #117625, .F. ) ;
#47203=ORIENTED_EDGE ( 'NONE', *, *, #81225, .F. ) ;
#47204=VERTEX_POINT ( 'NONE', #19601 ) ;
#47205=FACE_OUTER_BOUND ( 'NONE', #19722, .T. ) ;
#47207=VECTOR ( 'NONE', #16105, 1000.000000000000000 ) ;
#47210=ORIENTED_EDGE ( 'NONE', *, *, #61555, .F. ) ;
#47211=EDGE_LOOP ( 'NONE', ( #109626, #10147, #117359, #79530 ) ) ;
#47212=EDGE_CURVE ( 'NONE', #34241, #121192, #7993, .T. ) ;
#47213=DIRECTION ( 'NONE',  ( -0.7071067811865486830, 0.7071067811865464625, 0.000000000000000000 ) ) ;
#47214=ORIENTED_EDGE ( 'NONE', *, *, #45934, .T. ) ;
#47216=VECTOR ( 'NONE', #29197, 1000.000000000000000 ) ;
#47217=CARTESIAN_POINT ( 'NONE',  ( -15.18398860626900237, 28.73617430169797871, 5.000000000000000000 ) ) ;
#47218=LINE ( 'NONE', #68245, #89213 ) ;
#47219=DIRECTION ( 'NONE',  ( -0.7071067811865487940, 0.7071067811865463515, 0.000000000000000000 ) ) ;
#47220=EDGE_CURVE ( 'NONE', #80916, #119727, #73294, .T. ) ;
#47221=ORIENTED_EDGE ( 'NONE', *, *, #62266, .F. ) ;
#47223=DIRECTION ( 'NONE',  ( -1.000000000000000000, 0.000000000000000000, -0.000000000000000000 ) ) ;
#47224=CARTESIAN_POINT ( 'NONE',  ( -33.48921356237309510, -27.52281430457078670, 5.000000000000000000 ) ) ;
#47225=CARTESIAN_POINT ( 'NONE',  ( -22.03340032343008659, 6.759292476615653023, 12.28218704918517012 ) ) ;
#47226=CARTESIAN_POINT ( 'NONE',  ( -3.183988606268992161, 28.73617430169789699, 5.000000000000000000 ) ) ;
#47228=ADVANCED_FACE ( 'NONE', ( #97889 ), #8676, .F. ) ;
#47229=FACE_BOUND ( 'NONE', #74, .T. ) ;
#47230=ORIENTED_EDGE ( 'NONE', *, *, #26284, .F. ) ;
#47231=CARTESIAN_POINT ( 'NONE',  ( -32.99999999999977263, 7.007997736742408890, -8.085015511992185822 ) ) ;
#47232=DIRECTION ( 'NONE',  ( 0.7071067811865486830, -0.7071067811865464625, -0.000000000000000000 ) ) ;
#47233=VERTEX_POINT ( 'NONE', #119604 ) ;
#47234=CARTESIAN_POINT ( 'NONE',  ( -34.49999999999975131, -16.53574439159933718, 4.994342998332169437 ) ) ;
#47235=ORIENTED_EDGE ( 'NONE', *, *, #142685, .T. ) ;
#47236=EDGE_LOOP ( 'NONE', ( #106188, #30238, #107049, #3670 ) ) ;
#47240=EDGE_CURVE ( 'NONE', #27120, #94114, #142128, .T. ) ;
#47242=DIRECTION ( 'NONE',  ( -0.7071067811865486830, -0.7071067811865464625, 0.000000000000000000 ) ) ;
#47243=VECTOR ( 'NONE', #70942, 1000.000000000000227 ) ;
#47244=ORIENTED_EDGE ( 'NONE', *, *, #107014, .T. ) ;
#47245=CARTESIAN_POINT ( 'NONE',  ( 54.18398860626899705, 28.73617430169825226, 5.000000000000000000 ) ) ;
#47246=DIRECTION ( 'NONE',  ( 0.7071067811865487940, 0.7071067811865463515, 0.000000000000000000 ) ) ;
#47247=ORIENTED_EDGE ( 'NONE', *, *, #112637, .T. ) ;
#47248=VECTOR ( 'NONE', #70820, 1000.000000000000000 ) ;
#47249=ADVANCED_FACE ( 'NONE', ( #129790 ), #62422, .F. ) ;
#47251=EDGE_CURVE ( 'NONE', #29429, #36313, #84189, .T. ) ;
#47254=LINE ( 'NONE', #58842, #45943 ) ;
#47255=DIRECTION ( 'NONE',  ( -0.7071067811865486830, -0.7071067811865464625, 0.000000000000000000 ) ) ;
#47256=ORIENTED_EDGE ( 'NONE', *, *, #77225, .T. ) ;
#47257=ORIENTED_EDGE ( 'NONE', *, *, #66682, .T. ) ;
#47258=VECTOR ( 'NONE', #95174, 1000.000000000000227 ) ;
#47259=ORIENTED_EDGE ( 'NONE', *, *, #139079, .F. ) ;
#47260=ORIENTED_EDGE ( 'NONE', *, *, #21075, .T. ) ;
#47262=ORIENTED_EDGE ( 'NONE', *, *, #50725, .F. ) ;
#47263=ORIENTED_EDGE ( 'NONE', *, *, #113080, .T. ) ;
#47265=EDGE_CURVE ( 'NONE', #30447, #22650, #18138, .T. ) ;
#47266=LINE ( 'NONE', #2970, #101880 ) ;
#47267=ORIENTED_EDGE ( 'NONE', *, *, #112271, .F. ) ;
#47269=VERTEX_POINT ( 'NONE', #51543 ) ;
#47270=DIRECTION ( 'NONE',  ( 0.7071067811865487940, 0.7071067811865463515, 0.000000000000000000 ) ) ;
#47276=LINE ( 'NONE', #91447, #40667 ) ;
#47277=LINE ( 'NONE', #124070, #30377 ) ;
#47280=( NAMED_UNIT ( * ) SI_UNIT ( $, .STERADIAN. ) SOLID_ANGLE_UNIT ( ) );
#47281=DIRECTION ( 'NONE',  ( 1.000000000000000000, 0.000000000000000000, 0.000000000000000000 ) ) ;
#47282=EDGE_LOOP ( 'NONE', ( #109730, #30908, #81404, #104787 ) ) ;
#47283=DIRECTION ( 'NONE',  ( -0.000000000000000000, 0.3543493200069153248, 0.9351131265310292928 ) ) ;
#47284=DIRECTION ( 'NONE',  ( 0.6830127018922180770, -0.6830127018922204085, -0.2588190451025213501 ) ) ;
#47285=CARTESIAN_POINT ( 'NONE',  ( 26.35681257248245046, -20.24070752338406720, 21.22881796311218849 ) ) ;
#47286=CYLINDRICAL_SURFACE ( 'NONE', #95540, 0.5000000000000004441 ) ;
#47287=DIRECTION ( 'NONE',  ( 1.000000000000000000, 0.000000000000000000, 0.000000000000000000 ) ) ;
#47288=VECTOR ( 'NONE', #1317, 1000.000000000000227 ) ;
#47289=EDGE_LOOP ( 'NONE', ( #62786, #3998, #42147 ) ) ;
#47291=LINE ( 'NONE', #59561, #34952 ) ;
#47292=DIRECTION ( 'NONE',  ( 0.7071067811865486830, -0.7071067811865464625, -0.000000000000000000 ) ) ;
#47293=ORIENTED_EDGE ( 'NONE', *, *, #36660, .T. ) ;
#47294=CARTESIAN_POINT ( 'NONE',  ( -22.49999999999984013, -4.796895815301037480, -3.611700055028734813 ) ) ;
#47295=CARTESIAN_POINT ( 'NONE',  ( 14.99999999999989697, -12.03360074219761700, 5.000000000000000000 ) ) ;
#47296=ORIENTED_EDGE ( 'NONE', *, *, #118936, .F. ) ;
#47298=ORIENTED_EDGE ( 'NONE', *, *, #34666, .F. ) ;
#47299=EDGE_CURVE ( 'NONE', #86644, #116711, #139985, .T. ) ;
#47302=VECTOR ( 'NONE', #56150, 1000.000000000000000 ) ;
#47303=ORIENTED_EDGE ( 'NONE', *, *, #125732, .T. ) ;
#47304=ADVANCED_FACE ( 'NONE', ( #35523 ), #113021, .F. ) ;
#47305=EDGE_CURVE ( 'NONE', #64792, #33497, #118781, .T. ) ;
#47306=EDGE_CURVE ( 'NONE', #84441, #74571, #102182, .T. ) ;
#47307=VECTOR ( 'NONE', #63362, 1000.000000000000000 ) ;
#47308=DIRECTION ( 'NONE',  ( -0.7071067811865487940, 0.7071067811865463515, 0.000000000000000000 ) ) ;
#47312=EDGE_CURVE ( 'NONE', #129516, #46199, #13696, .T. ) ;
#47313=DIRECTION ( 'NONE',  ( -0.6830127018922181881, 0.6830127018922202975, -0.2588190451025214056 ) ) ;
#47314=DIRECTION ( 'NONE',  ( -0.7071067811865486830, -0.7071067811865464625, -0.000000000000000000 ) ) ;
#47315=DIRECTION ( 'NONE',  ( -0.000000000000000000, 0.000000000000000000, 1.000000000000000000 ) ) ;
#47316=PLANE ( 'NONE',  #85343 ) ;
#47319=FACE_OUTER_BOUND ( 'NONE', #89521, .T. ) ;
#47320=ORIENTED_EDGE ( 'NONE', *, *, #121085, .T. ) ;
#47321=VERTEX_POINT ( 'NONE', #77586 ) ;
#47322=VERTEX_POINT ( 'NONE', #11551 ) ;
#47324=ADVANCED_FACE ( 'NONE', ( #90589 ), #55106, .F. ) ;
#47325=VERTEX_POINT ( 'NONE', #12990 ) ;
#47326=VECTOR ( 'NONE', #100559, 1000.000000000000000 ) ;
#47327=VERTEX_POINT ( 'NONE', #66003 ) ;
#47328=VERTEX_POINT ( 'NONE', #121753 ) ;
#47330=CARTESIAN_POINT ( 'NONE',  ( -1.499999999999982236, -7.912538124160676922, 4.000000000000000000 ) ) ;
#47331=ORIENTED_EDGE ( 'NONE', *, *, #69726, .F. ) ;
#47334=VECTOR ( 'NONE', #85030, 1000.000000000000000 ) ;
#47335=EDGE_CURVE ( 'NONE', #23253, #27215, #19704, .T. ) ;
#47336=CARTESIAN_POINT ( 'NONE',  ( 27.48921356237309155, -27.52281430457074762, 5.000000000000000000 ) ) ;
#47337=VECTOR ( 'NONE', #70454, 1000.000000000000000 ) ;
#47341=CARTESIAN_POINT ( 'NONE',  ( 42.18398860626899705, 28.73617430169816700, 5.000000000000000000 ) ) ;
#47342=PLANE ( 'NONE',  #79272 ) ;
#47343=LINE ( 'NONE', #14654, #28834 ) ;
#47344=ADVANCED_FACE ( 'NONE', ( #21756 ), #22432, .F. ) ;
#47345=DIRECTION ( 'NONE',  ( 0.7071067811865487940, 0.7071067811865463515, 0.000000000000000000 ) ) ;
#47346=LINE ( 'NONE', #124841, #43525 ) ;
#47350=VECTOR ( 'NONE', #106361, 1000.000000000000000 ) ;
#47353=ORIENTED_EDGE ( 'NONE', *, *, #40526, .T. ) ;
#47354=ORIENTED_EDGE ( 'NONE', *, *, #11005, .T. ) ;
#47356=ORIENTED_EDGE ( 'NONE', *, *, #116834, .T. ) ;
#47357=ORIENTED_EDGE ( 'NONE', *, *, #130953, .F. ) ;
#47358=CARTESIAN_POINT ( 'NONE',  ( 19.49999999999986500, 22.22500000000000142, 4.362957392718781691 ) ) ;
#47359=CARTESIAN_POINT ( 'NONE',  ( 2.510786437626908008, -27.52281430457053446, 5.000000000000000000 ) ) ;
#47360=VERTEX_POINT ( 'NONE', #23903 ) ;
#47361=CARTESIAN_POINT ( 'NONE',  ( 0.000000000000000000, 0.000000000000000000, 5.000000000000000000 ) ) ;
#47362=CARTESIAN_POINT ( 'NONE',  ( -15.18398860626900237, 28.73617430169797871, 5.000000000000000000 ) ) ;
#47364=ORIENTED_EDGE ( 'NONE', *, *, #68016, .F. ) ;
#47365=EDGE_CURVE ( 'NONE', #42167, #15337, #110165, .T. ) ;
#47366=LINE ( 'NONE', #126292, #6249 ) ;
#47367=VERTEX_POINT ( 'NONE', #133385 ) ;
#47368=VECTOR ( 'NONE', #112320, 1000.000000000000000 ) ;
#47369=CARTESIAN_POINT ( 'NONE',  ( 19.49999999999987210, 16.46639925780209524, 5.000000000000000000 ) ) ;
#47370=LINE ( 'NONE', #922, #91669 ) ;
#47372=ADVANCED_FACE ( 'NONE', ( #112337 ), #89847, .T. ) ;
#47373=FACE_OUTER_BOUND ( 'NONE', #10942, .T. ) ;
#47374=ORIENTED_EDGE ( 'NONE', *, *, #90770, .F. ) ;
#47375=VERTEX_POINT ( 'NONE', #2090 ) ;
#47376=DIRECTION ( 'NONE',  ( -0.000000000000000000, 0.000000000000000000, 1.000000000000000000 ) ) ;
#47377=CARTESIAN_POINT ( 'NONE',  ( 14.52487387214945613, 14.25929247661557575, 9.797011795316668881 ) ) ;
#47378=CARTESIAN_POINT ( 'NONE',  ( 4.828169399223495084, 9.759292476615614831, 4.000000000000000000 ) ) ;
#47380=DIRECTION ( 'NONE',  ( 0.7071067811865487940, 0.7071067811865463515, -0.000000000000000000 ) ) ;
#47383=EDGE_CURVE ( 'NONE', #102967, #115135, #690, .T. ) ;
#47384=DIRECTION ( 'NONE',  ( 0.000000000000000000, 0.000000000000000000, 1.000000000000000000 ) ) ;
#47386=ORIENTED_EDGE ( 'NONE', *, *, #66725, .T. ) ;
#47388=VERTEX_POINT ( 'NONE', #44986 ) ;
#47389=AXIS2_PLACEMENT_3D ( 'NONE', #5953, #117570, #63951 ) ;
#47390=DIRECTION ( 'NONE',  ( -0.7071067811865486830, 0.7071067811865464625, 0.000000000000000000 ) ) ;
#47391=ORIENTED_EDGE ( 'NONE', *, *, #124617, .F. ) ;
#47393=CARTESIAN_POINT ( 'NONE',  ( 15.29974487139158867, -27.71228299555216879, 4.000000000000000000 ) ) ;
#47394=CARTESIAN_POINT ( 'NONE',  ( -34.45011844616454511, 22.22499999999999787, 4.231322045536046517 ) ) ;
#47396=EDGE_CURVE ( 'NONE', #80017, #11776, #89158, .T. ) ;
#47397=FACE_BOUND ( 'NONE', #122509, .T. ) ;
#47398=CARTESIAN_POINT ( 'NONE',  ( 12.48921356237309155, -27.52281430457064104, 5.000000000000000000 ) ) ;
#47399=ADVANCED_FACE ( 'NONE', ( #23143 ), #67423, .F. ) ;
#47401=ADVANCED_FACE ( 'NONE', ( #71693 ), #135525, .F. ) ;
#47402=DIRECTION ( 'NONE',  ( 0.7071067811865486830, -0.7071067811865464625, -0.000000000000000000 ) ) ;
#47403=VERTEX_POINT ( 'NONE', #138363 ) ;
#47404=VECTOR ( 'NONE', #142254, 1000.000000000000227 ) ;
#47405=CARTESIAN_POINT ( 'NONE',  ( 30.32816939922331656, -9.740707523384177335, 4.000000000000000000 ) ) ;
#47406=ORIENTED_EDGE ( 'NONE', *, *, #18175, .F. ) ;
#47407=ADVANCED_FACE ( 'NONE', ( #113752 ), #126075, .F. ) ;
#47410=ORIENTED_EDGE ( 'NONE', *, *, #53108, .T. ) ;
#47411=LINE ( 'NONE', #81444, #41798 ) ;
#47413=EDGE_LOOP ( 'NONE', ( #57267, #57269, #42413 ) ) ;
#47415=EDGE_CURVE ( 'NONE', #42016, #21974, #14447, .T. ) ;
#47416=PLANE ( 'NONE',  #95813 ) ;
#47417=ADVANCED_FACE ( 'NONE', ( #91317 ), #5677, .F. ) ;
#47418=CARTESIAN_POINT ( 'NONE',  ( 2.207106781186528810, -2.240707523384262601, 5.000000000000000000 ) ) ;
#47419=AXIS2_PLACEMENT_3D ( 'NONE', #73638, #62776, #19950 ) ;
#47420=CARTESIAN_POINT ( 'NONE',  ( 5.066132482466838560, -22.22500000000000142, 20.15413504464201822 ) ) ;
#47422=DIRECTION ( 'NONE',  ( 0.6830127018922180770, -0.6830127018922204085, -0.2588190451025213501 ) ) ;
#47423=LINE ( 'NONE', #134390, #74795 ) ;
#47424=DIRECTION ( 'NONE',  ( 1.000000000000000000, 0.000000000000000000, 0.000000000000000000 ) ) ;
#47425=ORIENTED_EDGE ( 'NONE', *, *, #67435, .F. ) ;
#47426=ORIENTED_EDGE ( 'NONE', *, *, #133847, .T. ) ;
#47427=CARTESIAN_POINT ( 'NONE',  ( -27.79289321881325492, 3.759292476615681888, 5.000000000000000000 ) ) ;
#47428=CARTESIAN_POINT ( 'NONE',  ( -9.183988606268997046, 28.73617430169793607, 5.000000000000000000 ) ) ;
#47429=ORIENTED_EDGE ( 'NONE', *, *, #114572, .F. ) ;
#47430=VERTEX_POINT ( 'NONE', #83271 ) ;
#47431=ORIENTED_EDGE ( 'NONE', *, *, #105092, .T. ) ;
#47432=EDGE_CURVE ( 'NONE', #30215, #14419, #26741, .T. ) ;
#47433=CARTESIAN_POINT ( 'NONE',  ( -34.92500000000001137, -22.22500000000000142, 4.500000000000000888 ) ) ;
#47434=ORIENTED_EDGE ( 'NONE', *, *, #89668, .T. ) ;
#47436=VECTOR ( 'NONE', #103204, 1000.000000000000000 ) ;
#47441=CARTESIAN_POINT ( 'NONE',  ( 2.999999999999983569, 16.93112307739200872, 4.000000000000000000 ) ) ;
#47442=EDGE_LOOP ( 'NONE', ( #54249, #69766, #38902, #76343 ) ) ;
#47443=VECTOR ( 'NONE', #78930, 1000.000000000000227 ) ;
#47444=LINE ( 'NONE', #59715, #124394 ) ;
#47445=PLANE ( 'NONE',  #53568 ) ;
#47446=DIRECTION ( 'NONE',  ( 0.7071067811865487940, -0.7071067811865463515, 0.000000000000000000 ) ) ;
#47447=LINE ( 'NONE', #48118, #24084 ) ;
#47448=ORIENTED_EDGE ( 'NONE', *, *, #74587, .F. ) ;
#47450=CARTESIAN_POINT ( 'NONE',  ( -36.29974487139159578, -27.71228299555231445, 4.000000000000000000 ) ) ;
#47451=DIRECTION ( 'NONE',  ( -1.000000000000000000, 0.000000000000000000, 0.000000000000000000 ) ) ;
#47452=DIRECTION ( 'NONE',  ( -0.000000000000000000, 0.3543493200069153248, 0.9351131265310292928 ) ) ;
#47453=ORIENTED_EDGE ( 'NONE', *, *, #132510, .T. ) ;
#47454=DIRECTION ( 'NONE',  ( 0.7071067811865487940, 0.7071067811865463515, -0.000000000000000000 ) ) ;
#47455=CARTESIAN_POINT ( 'NONE',  ( 33.29974487139158867, -27.71228299555229313, 4.000000000000000000 ) ) ;
#47457=DIRECTION ( 'NONE',  ( 1.000000000000000000, 0.000000000000000000, 0.000000000000000000 ) ) ;
#47458=EDGE_CURVE ( 'NONE', #126408, #48693, #127482, .T. ) ;
#47459=VERTEX_POINT ( 'NONE', #38342 ) ;
#47460=DIRECTION ( 'NONE',  ( 0.7071067811865487940, 0.7071067811865463515, -0.000000000000000000 ) ) ;
#47461=CARTESIAN_POINT ( 'NONE',  ( -2.700255128608413990, -27.71228299555204089, 4.000000000000000000 ) ) ;
#47464=DIRECTION ( 'NONE',  ( -0.7071067811865487940, 0.7071067811865463515, 0.000000000000000000 ) ) ;
#47465=ORIENTED_EDGE ( 'NONE', *, *, #71853, .F. ) ;
#47466=ORIENTED_EDGE ( 'NONE', *, *, #61575, .T. ) ;
#47468=CARTESIAN_POINT ( 'NONE',  ( -14.67183060077637080, -9.740707523384180888, 4.000000000000000000 ) ) ;
#47470=CARTESIAN_POINT ( 'NONE',  ( 34.92499999999998295, 14.93779483949076159, 7.761394445350724425 ) ) ;
#47471=EDGE_CURVE ( 'NONE', #141889, #115637, #70987, .T. ) ;
#47473=DIRECTION ( 'NONE',  ( -0.6830127018922181881, 0.6830127018922202975, -0.2588190451025214056 ) ) ;
#47474=LINE ( 'NONE', #124978, #23627 ) ;
#47476=EDGE_CURVE ( 'NONE', #33791, #116900, #80436, .T. ) ;
#47477=VERTEX_POINT ( 'NONE', #15814 ) ;
#47478=PLANE ( 'NONE',  #118255 ) ;
#47479=ADVANCED_FACE ( 'NONE', ( #125352 ), #25302, .F. ) ;
#47481=DIRECTION ( 'NONE',  ( 0.7071067811865487940, 0.7071067811865463515, 0.000000000000000000 ) ) ;
#47482=DIRECTION ( 'NONE',  ( 0.7071067811865487940, -0.7071067811865463515, 0.000000000000000000 ) ) ;
#47483=ADVANCED_FACE ( 'NONE', ( #58723 ), #4941, .F. ) ;
#47486=CARTESIAN_POINT ( 'NONE',  ( -1.499999999999994449, 3.073033219394623483, -6.593910359670974053 ) ) ;
#47488=ORIENTED_EDGE ( 'NONE', *, *, #12875, .T. ) ;
#47489=EDGE_CURVE ( 'NONE', #63122, #13922, #82558, .T. ) ;
#47490=LINE ( 'NONE', #36554, #69758 ) ;
#47491=VERTEX_POINT ( 'NONE', #107844 ) ;
#47492=LINE ( 'NONE', #134463, #10760 ) ;
#47494=CARTESIAN_POINT ( 'NONE',  ( 15.18398860626900237, 28.73617430169797871, 5.000000000000000000 ) ) ;
#47496=LINE ( 'NONE', #91658, #139002 ) ;
#47497=EDGE_CURVE ( 'NONE', #8014, #138855, #53501, .T. ) ;
#47498=DIRECTION ( 'NONE',  ( 0.000000000000000000, 1.000000000000000000, 0.000000000000000000 ) ) ;
#47499=ORIENTED_EDGE ( 'NONE', *, *, #143392, .F. ) ;
#47500=EDGE_LOOP ( 'NONE', ( #85772, #95415, #123666, #112548 ) ) ;
#47501=PLANE ( 'NONE',  #76485 ) ;
#47502=CARTESIAN_POINT ( 'NONE',  ( -29.99451991528749417, 28.92564299267958816, 4.000000000000000000 ) ) ;
#47504=LINE ( 'NONE', #26420, #17236 ) ;
#47505=EDGE_CURVE ( 'NONE', #98113, #86260, #97708, .T. ) ;
#47506=CARTESIAN_POINT ( 'NONE',  ( 57.48921356237308800, -27.52281430457095368, 5.000000000000000000 ) ) ;
#47508=DIRECTION ( 'NONE',  ( 0.3543493200069162685, -0.000000000000000000, -0.9351131265310288487 ) ) ;
#47510=CARTESIAN_POINT ( 'NONE',  ( 19.05000000000000071, 3.174999999999997158, 1.444000000000000394 ) ) ;
#47511=ORIENTED_EDGE ( 'NONE', *, *, #111962, .T. ) ;
#47515=CARTESIAN_POINT ( 'NONE',  ( -21.18398860626899349, 28.73617430169802134, 5.000000000000000000 ) ) ;
#47516=DIRECTION ( 'NONE',  ( 0.6830127018922181881, 0.6830127018922202975, -0.2588190451025214056 ) ) ;
#47517=ORIENTED_EDGE ( 'NONE', *, *, #116484, .T. ) ;
#47518=( BOUNDED_CURVE ( )  B_SPLINE_CURVE ( 3, ( #80337, #11621, #22498, #53762 ),
 .UNSPECIFIED., .F., .F. ) 
 B_SPLINE_CURVE_WITH_KNOTS ( ( 4, 4 ),
 ( 4.350170835173036821, 4.500739107949214279 ),
 .UNSPECIFIED. ) 
 CURVE ( )  GEOMETRIC_REPRESENTATION_ITEM ( )  RATIONAL_B_SPLINE_CURVE ( ( 1.000000000000000000, 0.9981116584018959736, 0.9981116584018959736, 1.000000000000000000 ) ) 
 REPRESENTATION_ITEM ( '' )  );
#47519=CARTESIAN_POINT ( 'NONE',  ( 28.49999999999980460, -19.91253812416055169, 4.000000000000000000 ) ) ;
#47524=LINE ( 'NONE', #14108, #15859 ) ;
#47525=VERTEX_POINT ( 'NONE', #30313 ) ;
#47526=VERTEX_POINT ( 'NONE', #84696 ) ;
#47527=( BOUNDED_CURVE ( )  B_SPLINE_CURVE ( 3, ( #71225, #16061, #27683, #104536 ),
 .UNSPECIFIED., .F., .F. ) 
 B_SPLINE_CURVE_WITH_KNOTS ( ( 4, 4 ),
 ( 1.964434688349488090, 3.503810798801450854 ),
 .UNSPECIFIED. ) 
 CURVE ( )  GEOMETRIC_REPRESENTATION_ITEM ( )  RATIONAL_B_SPLINE_CURVE ( ( 1.000000000000000000, 0.8120851936182283959, 0.8120851936182283959, 1.000000000000000000 ) ) 
 REPRESENTATION_ITEM ( '' )  );
#47529=CARTESIAN_POINT ( 'NONE',  ( 39.48921356237310221, -27.52281430457082934, 5.000000000000000000 ) ) ;
#47530=CARTESIAN_POINT ( 'NONE',  ( -25.49999999999981526, -14.94781430457066840, 5.000000000000000000 ) ) ;
#47531=CARTESIAN_POINT ( 'NONE',  ( -16.49999999999989342, 9.431123077392092213, 4.000000000000000000 ) ) ;
#47532=LINE ( 'NONE', #59117, #107758 ) ;
#47533=ORIENTED_EDGE ( 'NONE', *, *, #40111, .F. ) ;
#47537=CARTESIAN_POINT ( 'NONE',  ( -14.99451991528749595, 28.92564299267948513, 4.000000000000000000 ) ) ;
#47538=EDGE_LOOP ( 'NONE', ( #76041, #112520, #112474, #124834 ) ) ;
#47539=EDGE_CURVE ( 'NONE', #4808, #110593, #128899, .T. ) ;
#47541=ORIENTED_EDGE ( 'NONE', *, *, #138657, .T. ) ;
#47542=AXIS2_PLACEMENT_3D ( 'NONE', #40971, #107637, #43826 ) ;
#47543=AXIS2_PLACEMENT_3D ( 'NONE', #77375, #65056, #99058 ) ;
#47545=AXIS2_PLACEMENT_3D ( 'NONE', #55605, #99798, #470 ) ;
#47546=DIRECTION ( 'NONE',  ( 1.000000000000000000, 0.000000000000000000, 0.000000000000000000 ) ) ;
#47548=CARTESIAN_POINT ( 'NONE',  ( 9.707106781186471522, 20.25929247661551003, 5.000000000000000000 ) ) ;
#47549=EDGE_CURVE ( 'NONE', #48100, #58745, #139088, .T. ) ;
#47551=CARTESIAN_POINT ( 'NONE',  ( 60.48921356237309510, -27.52281430457097500, 5.000000000000000000 ) ) ;
#47552=ORIENTED_EDGE ( 'NONE', *, *, #116396, .F. ) ;
#47554=DIRECTION ( 'NONE',  ( -0.6830127018922180770, -0.6830127018922204085, -0.2588190451025213501 ) ) ;
#47557=EDGE_CURVE ( 'NONE', #18761, #118169, #105699, .T. ) ;
#47558=EDGE_LOOP ( 'NONE', ( #114047, #39078, #105900, #81951 ) ) ;
#47559=CARTESIAN_POINT ( 'NONE',  ( 21.18398860626899349, 28.73617430169802134, 5.000000000000000000 ) ) ;
#47560=CARTESIAN_POINT ( 'NONE',  ( 54.18398860626899705, 28.73617430169825226, 5.000000000000000000 ) ) ;
#47561=ORIENTED_EDGE ( 'NONE', *, *, #112562, .F. ) ;
#47562=EDGE_CURVE ( 'NONE', #28313, #55124, #39793, .T. ) ;
#47563=FACE_BOUND ( 'NONE', #98907, .T. ) ;
#47564=PLANE ( 'NONE',  #82640 ) ;
#47565=CARTESIAN_POINT ( 'NONE',  ( -8.816011393731004731, 28.73617430169781173, 5.000000000000000000 ) ) ;
#47567=LINE ( 'NONE', #91725, #85127 ) ;
#47569=ORIENTED_EDGE ( 'NONE', *, *, #8145, .T. ) ;
#47572=ORIENTED_EDGE ( 'NONE', *, *, #6380, .F. ) ;
#47573=DIRECTION ( 'NONE',  ( 0.7071067811865486830, -0.7071067811865464625, -0.000000000000000000 ) ) ;
#47574=FACE_OUTER_BOUND ( 'NONE', #93930, .T. ) ;
#47575=CARTESIAN_POINT ( 'NONE',  ( 34.92499999999998295, 22.22500000000000142, 4.000000000000000000 ) ) ;
#47576=CARTESIAN_POINT ( 'NONE',  ( -7.499999999999944933, 18.05218569542898877, 5.000000000000000000 ) ) ;
#47577=ORIENTED_EDGE ( 'NONE', *, *, #137365, .T. ) ;
#47578=FACE_OUTER_BOUND ( 'NONE', #119148, .T. ) ;
#47579=EDGE_CURVE ( 'NONE', #114819, #140054, #7826, .T. ) ;
#47580=DIRECTION ( 'NONE',  ( -0.7071067811865486830, 0.7071067811865464625, -0.000000000000000000 ) ) ;
#47581=EDGE_CURVE ( 'NONE', #88391, #91761, #84018, .T. ) ;
#47582=CARTESIAN_POINT ( 'NONE',  ( -20.99999999999984368, -22.06887692260758982, 4.000000000000000000 ) ) ;
#47584=CARTESIAN_POINT ( 'NONE',  ( -14.99999999999989519, 19.93112307739198386, 4.000000000000000000 ) ) ;
#47585=LINE ( 'NONE', #46142, #9689 ) ;
#47586=ORIENTED_EDGE ( 'NONE', *, *, #55937, .F. ) ;
#47587=CARTESIAN_POINT ( 'NONE',  ( 23.99999999999982947, -13.44781430457068261, 5.000000000000000000 ) ) ;
#47588=DIRECTION ( 'NONE',  ( 0.6830127018922181881, 0.6830127018922202975, -0.2588190451025214056 ) ) ;
#47592=ADVANCED_FACE ( 'NONE', ( #41178 ), #52759, .F. ) ;
#47593=ORIENTED_EDGE ( 'NONE', *, *, #52146, .F. ) ;
#47595=ORIENTED_EDGE ( 'NONE', *, *, #128938, .T. ) ;
#47596=AXIS2_PLACEMENT_3D ( 'NONE', #106273, #63561, #95428 ) ;
#47598=CARTESIAN_POINT ( 'NONE',  ( 0.000000000000000000, 21.72500000000000142, 4.500000000000000888 ) ) ;
#47599=VERTEX_POINT ( 'NONE', #41919 ) ;
#47601=LINE ( 'NONE', #27214, #108112 ) ;
#47602=VERTEX_POINT ( 'NONE', #86129 ) ;
#47606=ORIENTED_EDGE ( 'NONE', *, *, #38469, .F. ) ;
#47607=EDGE_CURVE ( 'NONE', #100760, #90138, #20128, .T. ) ;
#47608=PLANE ( 'NONE',  #26024 ) ;
#47609=CARTESIAN_POINT ( 'NONE',  ( -14.99999999999989519, -8.731860332648849976, -2.120594902707574558 ) ) ;
#47610=PLANE ( 'NONE',  #96109 ) ;
#47611=ORIENTED_EDGE ( 'NONE', *, *, #81642, .T. ) ;
#47613=AXIS2_PLACEMENT_3D ( 'NONE', #133228, #44820, #99857 ) ;
#47615=ORIENTED_EDGE ( 'NONE', *, *, #65779, .T. ) ;
#47616=ORIENTED_EDGE ( 'NONE', *, *, #63618, .F. ) ;
#47618=DIRECTION ( 'NONE',  ( -0.7071067811865486830, 0.7071067811865464625, 0.000000000000000000 ) ) ;
#47619=FACE_OUTER_BOUND ( 'NONE', #3370, .T. ) ;
#47620=CARTESIAN_POINT ( 'NONE',  ( -60.48921356237309510, -27.52281430457097500, 5.000000000000000000 ) ) ;
#47621=DIRECTION ( 'NONE',  ( -0.7071067811865487940, 0.7071067811865463515, 0.000000000000000000 ) ) ;
#47622=ORIENTED_EDGE ( 'NONE', *, *, #65379, .F. ) ;
#47625=CARTESIAN_POINT ( 'NONE',  ( -5.999999999999951150, -1.447814304570816946, 5.000000000000000000 ) ) ;
#47626=VECTOR ( 'NONE', #67097, 1000.000000000000000 ) ;
#47627=ADVANCED_FACE ( 'NONE', ( #112176 ), #89000, .F. ) ;
#47628=DIRECTION ( 'NONE',  ( -0.3543493200069162685, -0.000000000000000000, -0.9351131265310288487 ) ) ;
#47629=VECTOR ( 'NONE', #34729, 1000.000000000000000 ) ;
#47630=LINE ( 'NONE', #125879, #4957 ) ;
#47631=EDGE_LOOP ( 'NONE', ( #120194, #60421, #24841, #54499 ) ) ;
#47632=EDGE_CURVE ( 'NONE', #23928, #927, #1916, .T. ) ;
#47633=ORIENTED_EDGE ( 'NONE', *, *, #109080, .T. ) ;
#47634=ORIENTED_EDGE ( 'NONE', *, *, #36629, .T. ) ;
#47635=CARTESIAN_POINT ( 'NONE',  ( 14.28242261357422294, -21.73023691814493219, 5.000000000000000888 ) ) ;
#47636=FACE_OUTER_BOUND ( 'NONE', #45602, .T. ) ;
#47638=DIRECTION ( 'NONE',  ( -0.6830127018922180770, -0.6830127018922204085, -0.2588190451025213501 ) ) ;
#47639=AXIS2_PLACEMENT_3D ( 'NONE', #98947, #75801, #142486 ) ;
#47640=LINE ( 'NONE', #101972, #72879 ) ;
#47641=PLANE ( 'NONE',  #101430 ) ;
#47642=EDGE_CURVE ( 'NONE', #3113, #111037, #56400, .T. ) ;
#47643=CARTESIAN_POINT ( 'NONE',  ( -17.67183060077634948, 17.25929247661553845, 4.000000000000000000 ) ) ;
#47644=EDGE_CURVE ( 'NONE', #98880, #140231, #12115, .T. ) ;
#47646=CARTESIAN_POINT ( 'NONE',  ( -72.29974487139158157, -27.71228299555256669, 4.000000000000000000 ) ) ;
#47647=CARTESIAN_POINT ( 'NONE',  ( -21.18398860626899349, 28.73617430169802134, 5.000000000000000000 ) ) ;
#47648=LINE ( 'NONE', #80259, #120643 ) ;
#47650=ORIENTED_EDGE ( 'NONE', *, *, #31902, .T. ) ;
#47652=VERTEX_POINT ( 'NONE', #54937 ) ;
#47653=CARTESIAN_POINT ( 'NONE',  ( -39.48921356237310221, -27.52281430457082934, 5.000000000000000000 ) ) ;
#47655=ORIENTED_EDGE ( 'NONE', *, *, #235, .T. ) ;
#47656=ADVANCED_FACE ( 'NONE', ( #66524 ), #143351, .F. ) ;
#47658=DIRECTION ( 'NONE',  ( 0.7071067811865486830, -0.7071067811865464625, -0.000000000000000000 ) ) ;
#47659=LINE ( 'NONE', #80968, #5565 ) ;
#47660=VERTEX_POINT ( 'NONE', #11372 ) ;
#47661=DIRECTION ( 'NONE',  ( -0.7071067811865486830, -0.7071067811865464625, 0.000000000000000000 ) ) ;
#47662=VERTEX_POINT ( 'NONE', #98428 ) ;
#47665=EDGE_LOOP ( 'NONE', ( #122681, #41223, #106086, #35778 ) ) ;
#47666=LINE ( 'NONE', #91826, #133279 ) ;
#47669=LINE ( 'NONE', #126589, #81016 ) ;
#47670=CARTESIAN_POINT ( 'NONE',  ( -33.18398860626899705, 28.73617430169810305, 5.000000000000000000 ) ) ;
#47671=ORIENTED_EDGE ( 'NONE', *, *, #92785, .T. ) ;
#47672=DIRECTION ( 'NONE',  ( -0.000000000000000000, -0.3543493200069152138, 0.9351131265310292928 ) ) ;
#47673=DIRECTION ( 'NONE',  ( -0.7071067811865486830, 0.7071067811865464625, 0.000000000000000000 ) ) ;
#47674=DIRECTION ( 'NONE',  ( 0.6830127018922180770, -0.6830127018922204085, -0.2588190451025213501 ) ) ;
#47677=ADVANCED_FACE ( 'NONE', ( #65110 ), #32468, .F. ) ;
#47678=CARTESIAN_POINT ( 'NONE',  ( 9.299744871391588674, -27.71228299555212971, 4.000000000000000000 ) ) ;
#47679=LINE ( 'NONE', #57114, #101083 ) ;
#47680=ORIENTED_EDGE ( 'NONE', *, *, #69709, .F. ) ;
#47681=CARTESIAN_POINT ( 'NONE',  ( 20.81601139373100295, 28.73617430169773002, 5.000000000000000000 ) ) ;
#47682=ORIENTED_EDGE ( 'NONE', *, *, #116005, .T. ) ;
#47684=DIRECTION ( 'NONE',  ( 0.6830127018922181881, 0.6830127018922202975, -0.2588190451025214056 ) ) ;
#47685=DIRECTION ( 'NONE',  ( 0.7071067811865487940, -0.7071067811865463515, 0.000000000000000000 ) ) ;
#47689=ORIENTED_EDGE ( 'NONE', *, *, #66863, .T. ) ;
#47690=CARTESIAN_POINT ( 'NONE',  ( -17.99999999999987210, -21.84840872380826227, 2.849755605029565597 ) ) ;
#47691=LINE ( 'NONE', #100613, #21061 ) ;
#47692=VERTEX_POINT ( 'NONE', #120876 ) ;
#47693=PLANE ( 'NONE',  #6869 ) ;
#47694=DIRECTION ( 'NONE',  ( 0.7071067811865487940, 0.7071067811865463515, 0.000000000000000000 ) ) ;
#47695=CARTESIAN_POINT ( 'NONE',  ( -9.183988606268997046, 28.73617430169793607, 5.000000000000000000 ) ) ;
#47696=ORIENTED_EDGE ( 'NONE', *, *, #121359, .F. ) ;
#47697=EDGE_CURVE ( 'NONE', #73610, #9196, #21586, .T. ) ;
#47698=DIRECTION ( 'NONE',  ( -0.3543493200069162685, -0.000000000000000000, -0.9351131265310288487 ) ) ;
#47699=EDGE_CURVE ( 'NONE', #109689, #94631, #111434, .T. ) ;
#47700=DIRECTION ( 'NONE',  ( 0.3543493200069162685, -0.000000000000000000, -0.9351131265310288487 ) ) ;
#47702=DIRECTION ( 'NONE',  ( -0.7071067811865486830, -0.7071067811865464625, -0.000000000000000000 ) ) ;
#47706=ORIENTED_EDGE ( 'NONE', *, *, #119601, .T. ) ;
#47707=ORIENTED_EDGE ( 'NONE', *, *, #128639, .T. ) ;
#47709=EDGE_LOOP ( 'NONE', ( #17248, #81773, #129140, #38124 ) ) ;
#47710=VECTOR ( 'NONE', #132940, 1000.000000000000000 ) ;
#47711=DIRECTION ( 'NONE',  ( 1.000000000000000000, -0.000000000000000000, -0.000000000000000000 ) ) ;
#47712=DIRECTION ( 'NONE',  ( 0.7071067811865487940, 0.7071067811865463515, -0.000000000000000000 ) ) ;
#47713=PLANE ( 'NONE',  #140603 ) ;
#47714=FACE_OUTER_BOUND ( 'NONE', #141144, .T. ) ;
#47715=ORIENTED_EDGE ( 'NONE', *, *, #7625, .F. ) ;
#47718=LINE ( 'NONE', #23787, #2402 ) ;
#47721=VECTOR ( 'NONE', #14081, 1000.000000000000000 ) ;
#47722=CARTESIAN_POINT ( 'NONE',  ( -30.18398860626900060, 28.73617430169808173, 5.000000000000000000 ) ) ;
#47723=DIRECTION ( 'NONE',  ( -0.000000000000000000, 0.3543493200069153248, 0.9351131265310292928 ) ) ;
#47724=DIRECTION ( 'NONE',  ( 0.7071067811865487940, 0.7071067811865463515, -0.000000000000000000 ) ) ;
#47725=ORIENTED_EDGE ( 'NONE', *, *, #15532, .F. ) ;
#47726=VERTEX_POINT ( 'NONE', #27273 ) ;
#47727=DIRECTION ( 'NONE',  ( 0.3543493200069162685, -0.000000000000000000, -0.9351131265310288487 ) ) ;
#47729=PLANE ( 'NONE',  #69730 ) ;
#47731=LINE ( 'NONE', #1302, #41796 ) ;
#47732=CARTESIAN_POINT ( 'NONE',  ( 51.48921356237309510, -27.52281430457091460, 5.000000000000000000 ) ) ;
#47734=VECTOR ( 'NONE', #50339, 1000.000000000000000 ) ;
#47735=ORIENTED_EDGE ( 'NONE', *, *, #141042, .F. ) ;
#47736=ORIENTED_EDGE ( 'NONE', *, *, #87063, .F. ) ;
#47737=VECTOR ( 'NONE', #131269, 999.9999999999998863 ) ;
#47738=LINE ( 'NONE', #91903, #117398 ) ;
#47739=EDGE_CURVE ( 'NONE', #34380, #63020, #48332, .T. ) ;
#47740=ORIENTED_EDGE ( 'NONE', *, *, #41251, .F. ) ;
#47741=VECTOR ( 'NONE', #44635, 999.9999999999998863 ) ;
#47742=DIRECTION ( 'NONE',  ( 0.6830127018922180770, -0.6830127018922204085, -0.2588190451025213501 ) ) ;
#47744=DIRECTION ( 'NONE',  ( 0.7071067811865487940, 0.7071067811865463515, 0.000000000000000000 ) ) ;
#47745=FACE_OUTER_BOUND ( 'NONE', #43673, .T. ) ;
#47747=DIRECTION ( 'NONE',  ( -0.6830127018922181881, 0.6830127018922202975, -0.2588190451025214056 ) ) ;
#47748=VERTEX_POINT ( 'NONE', #106794 ) ;
#47749=LINE ( 'NONE', #76247, #130465 ) ;
#47751=ORIENTED_EDGE ( 'NONE', *, *, #101327, .F. ) ;
#47752=EDGE_CURVE ( 'NONE', #61225, #82235, #58553, .T. ) ;
#47753=CARTESIAN_POINT ( 'NONE',  ( -7.828169399223476432, 9.759292476615614831, 4.000000000000000000 ) ) ;
#47754=ORIENTED_EDGE ( 'NONE', *, *, #11254, .F. ) ;
#47755=ORIENTED_EDGE ( 'NONE', *, *, #7281, .T. ) ;
#47756=CARTESIAN_POINT ( 'NONE',  ( 0.3281693992235311108, -9.740707523384182664, 4.000000000000000000 ) ) ;
#47757=EDGE_CURVE ( 'NONE', #2221, #134621, #113571, .T. ) ;
#47758=VERTEX_POINT ( 'NONE', #125177 ) ;
#47759=VERTEX_POINT ( 'NONE', #14268 ) ;
#47760=DIRECTION ( 'NONE',  ( 0.6830127018922180770, -0.6830127018922204085, -0.2588190451025213501 ) ) ;
#47761=ORIENTED_EDGE ( 'NONE', *, *, #54570, .F. ) ;
#47762=LINE ( 'NONE', #93368, #109032 ) ;
#47763=DIRECTION ( 'NONE',  ( 0.3543493200069162685, -0.000000000000000000, -0.9351131265310288487 ) ) ;
#47766=EDGE_CURVE ( 'NONE', #72201, #92747, #114294, .T. ) ;
#47767=PLANE ( 'NONE',  #106054 ) ;
#47769=DIRECTION ( 'NONE',  ( 0.6830127018922180770, -0.6830127018922204085, -0.2588190451025214056 ) ) ;
#47771=VECTOR ( 'NONE', #120737, 1000.000000000000000 ) ;
#47772=DIRECTION ( 'NONE',  ( 1.000000000000000000, 0.000000000000000000, 0.000000000000000000 ) ) ;
#47774=CARTESIAN_POINT ( 'NONE',  ( 3.792893218813436551, -17.24070752338410628, 5.000000000000000000 ) ) ;
#47775=ORIENTED_EDGE ( 'NONE', *, *, #116149, .F. ) ;
#47776=PLANE ( 'NONE',  #94335 ) ;
#47777=DIRECTION ( 'NONE',  ( -0.7071067811865486830, -0.7071067811865464625, -0.000000000000000000 ) ) ;
#47778=ORIENTED_EDGE ( 'NONE', *, *, #10541, .T. ) ;
#47780=AXIS2_PLACEMENT_3D ( 'NONE', #336, #109116, #64205 ) ;
#47781=PLANE ( 'NONE',  #118882 ) ;
#47782=EDGE_CURVE ( 'NONE', #51950, #102894, #3367, .T. ) ;
#47783=ORIENTED_EDGE ( 'NONE', *, *, #78402, .T. ) ;
#47784=CARTESIAN_POINT ( 'NONE',  ( 26.99999999999981526, -18.03360074219755660, 5.000000000000000000 ) ) ;
#47788=ORIENTED_EDGE ( 'NONE', *, *, #4380, .F. ) ;
#47789=DIRECTION ( 'NONE',  ( 0.7071067811865487940, 0.7071067811865463515, 0.000000000000000000 ) ) ;
#47790=ORIENTED_EDGE ( 'NONE', *, *, #7824, .F. ) ;
#47791=CARTESIAN_POINT ( 'NONE',  ( 17.67183060077634948, -15.74070752338412049, 4.000000000000000000 ) ) ;
#47792=VECTOR ( 'NONE', #93882, 1000.000000000000000 ) ;
#47795=VECTOR ( 'NONE', #138989, 1000.000000000000000 ) ;
#47797=ORIENTED_EDGE ( 'NONE', *, *, #121366, .F. ) ;
#47798=EDGE_CURVE ( 'NONE', #78244, #91252, #91822, .T. ) ;
#47800=ORIENTED_EDGE ( 'NONE', *, *, #8204, .T. ) ;
#47803=LINE ( 'NONE', #134808, #75159 ) ;
#47804=DIRECTION ( 'NONE',  ( -0.6830127018922181881, 0.6830127018922202975, -0.2588190451025214056 ) ) ;
#47805=VERTEX_POINT ( 'NONE', #92524 ) ;
#47806=DIRECTION ( 'NONE',  ( -0.000000000000000000, 0.3543493200069153248, 0.9351131265310292928 ) ) ;
#47808=EDGE_CURVE ( 'NONE', #131497, #91250, #60684, .T. ) ;
#47809=PLANE ( 'NONE',  #45785 ) ;
#47810=AXIS2_PLACEMENT_3D ( 'NONE', #99760, #30966, #132441 ) ;
#47811=DIRECTION ( 'NONE',  ( -1.000000000000000000, 0.000000000000000000, 0.000000000000000000 ) ) ;
#47812=PLANE ( 'NONE',  #93154 ) ;
#47813=ORIENTED_EDGE ( 'NONE', *, *, #96770, .F. ) ;
#47815=EDGE_CURVE ( 'NONE', #48369, #45681, #136754, .T. ) ;
#47816=EDGE_LOOP ( 'NONE', ( #49832, #78161, #77879, #3957 ) ) ;
#47819=VECTOR ( 'NONE', #31097, 1000.000000000000000 ) ;
#47820=ADVANCED_FACE ( 'NONE', ( #37471 ), #36730, .F. ) ;
#47822=ADVANCED_FACE ( 'NONE', ( #112860 ), #13529, .T. ) ;
#47823=DIRECTION ( 'NONE',  ( 0.7071067811865487940, -0.7071067811865463515, 0.000000000000000000 ) ) ;
#47824=DIRECTION ( 'NONE',  ( 0.7071067811865487940, 0.7071067811865463515, 0.000000000000000000 ) ) ;
#47825=ORIENTED_EDGE ( 'NONE', *, *, #108097, .T. ) ;
#47828=VERTEX_POINT ( 'NONE', #81706 ) ;
#47829=AXIS2_PLACEMENT_3D ( 'NONE', #48929, #49659, #72136 ) ;
#47830=VECTOR ( 'NONE', #42354, 999.9999999999998863 ) ;
#47832=CARTESIAN_POINT ( 'NONE',  ( 10.49999999999992184, 8.900465351122159419, -2.516491619111538292 ) ) ;
#47833=VECTOR ( 'NONE', #47886, 999.9999999999998863 ) ;
#47835=DIRECTION ( 'NONE',  ( -2.781805975412905890E-17, 0.3543493200069152693, 0.9351131265310292928 ) ) ;
#47836=ADVANCED_FACE ( 'NONE', ( #57809 ), #38185, .F. ) ;
#47837=CARTESIAN_POINT ( 'NONE',  ( 11.81601139373100651, 28.73617430169779041, 5.000000000000000000 ) ) ;
#47838=DIRECTION ( 'NONE',  ( -0.7071067811865486830, -0.7071067811865464625, 0.000000000000000000 ) ) ;
#47839=DIRECTION ( 'NONE',  ( 0.7071067811865486830, -0.7071067811865464625, -0.000000000000000000 ) ) ;
#47840=CARTESIAN_POINT ( 'NONE',  ( 54.48921356237310221, -27.52281430457093236, 5.000000000000000000 ) ) ;
#47841=DIRECTION ( 'NONE',  ( 0.6830127018922181881, 0.6830127018922202975, -0.2588190451025214056 ) ) ;
#47844=DIRECTION ( 'NONE',  ( -0.000000000000000000, -0.3543493200069152693, 0.9351131265310292928 ) ) ;
#47846=ADVANCED_FACE ( 'NONE', ( #80271 ), #15650, .F. ) ;
#47847=FACE_OUTER_BOUND ( 'NONE', #127529, .T. ) ;
#47848=LINE ( 'NONE', #4960, #114827 ) ;
#47849=EDGE_LOOP ( 'NONE', ( #6182, #138321, #26417, #123037 ) ) ;
#47850=ORIENTED_EDGE ( 'NONE', *, *, #20646, .F. ) ;
#47852=EDGE_LOOP ( 'NONE', ( #44046, #119937, #127545, #30968 ) ) ;
#47853=ORIENTED_EDGE ( 'NONE', *, *, #3567, .T. ) ;
#47859=PLANE ( 'NONE',  #69585 ) ;
#47860=DIRECTION ( 'NONE',  ( 0.7071067811865487940, -0.7071067811865463515, 0.000000000000000000 ) ) ;
#47862=DIRECTION ( 'NONE',  ( 0.7071067811865487940, 0.7071067811865463515, 0.000000000000000000 ) ) ;
#47864=EDGE_CURVE ( 'NONE', #51050, #86215, #82401, .T. ) ;
#47865=DIRECTION ( 'NONE',  ( 0.7071067811865486830, -0.7071067811865464625, -0.000000000000000000 ) ) ;
#47866=DIRECTION ( 'NONE',  ( -0.7071067811865486830, 0.7071067811865464625, 0.000000000000000000 ) ) ;
#47867=CARTESIAN_POINT ( 'NONE',  ( 11.99999999999992006, -10.44781430457072346, 5.000000000000000000 ) ) ;
#47869=ADVANCED_FACE ( 'NONE', ( #75624 ), #64736, .F. ) ;
#47870=EDGE_CURVE ( 'NONE', #39265, #126191, #131430, .T. ) ;
#47871=ORIENTED_EDGE ( 'NONE', *, *, #47632, .F. ) ;
#47872=EDGE_LOOP ( 'NONE', ( #32994, #139745, #111772, #113215 ) ) ;
#47874=ORIENTED_EDGE ( 'NONE', *, *, #33839, .F. ) ;
#47875=DIRECTION ( 'NONE',  ( -0.7071067811865487940, 0.7071067811865463515, -0.000000000000000000 ) ) ;
#47876=VECTOR ( 'NONE', #71936, 1000.000000000000000 ) ;
#47877=ORIENTED_EDGE ( 'NONE', *, *, #69073, .T. ) ;
#47878=EDGE_CURVE ( 'NONE', #7505, #28061, #42298, .T. ) ;
#47879=DIRECTION ( 'NONE',  ( -0.000000000000000000, 0.000000000000000000, 1.000000000000000000 ) ) ;
#47883=ORIENTED_EDGE ( 'NONE', *, *, #21627, .F. ) ;
#47884=DIRECTION ( 'NONE',  ( -0.7071067811865486830, 0.7071067811865464625, 0.000000000000000000 ) ) ;
#47885=VECTOR ( 'NONE', #114802, 1000.000000000000000 ) ;
#47886=DIRECTION ( 'NONE',  ( -0.7071067811865487940, 0.7071067811865463515, -0.000000000000000000 ) ) ;
#47889=VECTOR ( 'NONE', #137927, 1000.000000000000000 ) ;
#47891=LINE ( 'NONE', #136281, #88537 ) ;
#47893=AXIS2_PLACEMENT_3D ( 'NONE', #254, #45960, #90144 ) ;
#47896=ORIENTED_EDGE ( 'NONE', *, *, #112306, .F. ) ;
#47898=CARTESIAN_POINT ( 'NONE',  ( -23.99999999999983302, -1.068876922607798985, 4.000000000000000000 ) ) ;
#47899=ORIENTED_EDGE ( 'NONE', *, *, #15024, .T. ) ;
#47900=EDGE_CURVE ( 'NONE', #771, #15594, #21228, .T. ) ;
#47901=ORIENTED_EDGE ( 'NONE', *, *, #3377, .F. ) ;
#47902=CARTESIAN_POINT ( 'NONE',  ( 30.48921356237309510, -27.52281430457076894, 5.000000000000000000 ) ) ;
#47903=LINE ( 'NONE', #36290, #112389 ) ;
#47904=CARTESIAN_POINT ( 'NONE',  ( -3.299744871391591339, -27.71228299555208352, 4.000000000000000000 ) ) ;
#47905=ORIENTED_EDGE ( 'NONE', *, *, #142999, .T. ) ;
#47906=CARTESIAN_POINT ( 'NONE',  ( -16.49999999999987566, -14.94781430457067906, 5.000000000000000000 ) ) ;
#47907=CARTESIAN_POINT ( 'NONE',  ( 13.58990935480160189, 9.759292476615618384, 11.28811694763781937 ) ) ;
#47908=CARTESIAN_POINT ( 'NONE',  ( 7.499999999999947597, 9.431123077392085108, 4.000000000000000000 ) ) ;
#47909=PLANE ( 'NONE',  #39738 ) ;
#47910=EDGE_CURVE ( 'NONE', #22767, #124122, #133626, .T. ) ;
#47911=VECTOR ( 'NONE', #75164, 1000.000000000000000 ) ;
#47912=FACE_BOUND ( 'NONE', #40057, .T. ) ;
#47914=CARTESIAN_POINT ( 'NONE',  ( 12.48921356237309155, -27.52281430457064104, 5.000000000000000000 ) ) ;
#47915=EDGE_CURVE ( 'NONE', #45336, #124524, #108923, .T. ) ;
#47917=CARTESIAN_POINT ( 'NONE',  ( 12.70710678118646619, 11.25929247661560240, 5.000000000000000000 ) ) ;
#47918=ORIENTED_EDGE ( 'NONE', *, *, #122635, .T. ) ;
#47919=CARTESIAN_POINT ( 'NONE',  ( 3.792893218813431666, -20.24070752338406720, 5.000000000000000000 ) ) ;
#47920=ORIENTED_EDGE ( 'NONE', *, *, #49890, .T. ) ;
#47921=EDGE_LOOP ( 'NONE', ( #88869, #68972, #118736, #36362 ) ) ;
#47922=VECTOR ( 'NONE', #50534, 999.9999999999998863 ) ;
#47924=VECTOR ( 'NONE', #97970, 1000.000000000000000 ) ;
#47925=EDGE_CURVE ( 'NONE', #32684, #63590, #129996, .T. ) ;
#47926=ADVANCED_FACE ( 'NONE', ( #98085 ), #87204, .F. ) ;
#47928=ORIENTED_EDGE ( 'NONE', *, *, #96361, .F. ) ;
#47929=FACE_OUTER_BOUND ( 'NONE', #12770, .T. ) ;
#47932=ADVANCED_FACE ( 'NONE', ( #32109 ), #65487, .F. ) ;
#47933=AXIS2_PLACEMENT_3D ( 'NONE', #65153, #42687, #76003 ) ;
#47934=VERTEX_POINT ( 'NONE', #66182 ) ;
#47936=AXIS2_PLACEMENT_3D ( 'NONE', #31436, #138777, #42328 ) ;
#47938=EDGE_CURVE ( 'NONE', #124700, #76836, #120499, .T. ) ;
#47939=DIRECTION ( 'NONE',  ( -0.7071067811865486830, -0.7071067811865464625, -0.000000000000000000 ) ) ;
#47941=CARTESIAN_POINT ( 'NONE',  ( -21.32816939922337340, -21.74070752338406720, 4.000000000000000000 ) ) ;
#47942=EDGE_LOOP ( 'NONE', ( #111170, #65722, #82354, #123616 ) ) ;
#47943=ORIENTED_EDGE ( 'NONE', *, *, #54761, .F. ) ;
#47944=ORIENTED_EDGE ( 'NONE', *, *, #18086, .T. ) ;
#47945=ORIENTED_EDGE ( 'NONE', *, *, #121644, .F. ) ;
#47946=LINE ( 'NONE', #2965, #88759 ) ;
#47947=EDGE_CURVE ( 'NONE', #115169, #79668, #109664, .T. ) ;
#47948=ORIENTED_EDGE ( 'NONE', *, *, #115973, .T. ) ;
#47949=ORIENTED_EDGE ( 'NONE', *, *, #111587, .F. ) ;
#47950=DIRECTION ( 'NONE',  ( 0.000000000000000000, 1.000000000000000000, 0.000000000000000000 ) ) ;
#47951=DIRECTION ( 'NONE',  ( -0.3543493200069162685, -0.000000000000000000, -0.9351131265310288487 ) ) ;
#47952=EDGE_LOOP ( 'NONE', ( #102106, #118844, #50111, #117548 ) ) ;
#47953=AXIS2_PLACEMENT_3D ( 'NONE', #70070, #15588, #4700 ) ;
#47954=LINE ( 'NONE', #113157, #55717 ) ;
#47955=ADVANCED_FACE ( 'NONE', ( #143009 ), #19087, .T. ) ;
#47960=ORIENTED_EDGE ( 'NONE', *, *, #134580, .F. ) ;
#47962=FACE_OUTER_BOUND ( 'NONE', #71264, .T. ) ;
#47963=DIRECTION ( 'NONE',  ( -0.000000000000000000, 0.000000000000000000, 1.000000000000000000 ) ) ;
#47964=CARTESIAN_POINT ( 'NONE',  ( 42.48921356237308800, -27.52281430457085065, 5.000000000000000000 ) ) ;
#47966=EDGE_CURVE ( 'NONE', #113044, #53162, #64030, .T. ) ;
#47967=VERTEX_POINT ( 'NONE', #29947 ) ;
#47968=FACE_OUTER_BOUND ( 'NONE', #50003, .T. ) ;
#47971=CARTESIAN_POINT ( 'NONE',  ( -26.01844734635654888, 18.75929247661551713, 20.33588619593448854 ) ) ;
#47972=CARTESIAN_POINT ( 'NONE',  ( 51.48921356237309510, -27.52281430457091460, 5.000000000000000000 ) ) ;
#47976=EDGE_CURVE ( 'NONE', #117979, #135052, #8178, .T. ) ;
#47977=VECTOR ( 'NONE', #85762, 1000.000000000000227 ) ;
#47979=CARTESIAN_POINT ( 'NONE',  ( 18.83652871126538386, 15.75929247661555799, 9.299976744542963303 ) ) ;
#47980=ADVANCED_FACE ( 'NONE', ( #19791 ), #108198, .T. ) ;
#47981=ORIENTED_EDGE ( 'NONE', *, *, #70464, .F. ) ;
#47983=VERTEX_POINT ( 'NONE', #47330 ) ;
#47986=ORIENTED_EDGE ( 'NONE', *, *, #101670, .F. ) ;
#47988=DIRECTION ( 'NONE',  ( 0.7071067811865487940, 0.7071067811865463515, -0.000000000000000000 ) ) ;
#47989=VECTOR ( 'NONE', #123511, 999.9999999999998863 ) ;
#47990=VERTEX_POINT ( 'NONE', #78478 ) ;
#47993=LINE ( 'NONE', #56750, #88275 ) ;
#47994=LINE ( 'NONE', #50828, #123063 ) ;
#47995=LINE ( 'NONE', #80614, #26258 ) ;
#47996=DIRECTION ( 'NONE',  ( 1.000000000000000000, 0.000000000000000000, 0.000000000000000000 ) ) ;
#47997=PLANE ( 'NONE',  #20483 ) ;
#47999=DIRECTION ( 'NONE',  ( 0.6830127018922181881, 0.6830127018922202975, -0.2588190451025214056 ) ) ;
#48001=ORIENTED_EDGE ( 'NONE', *, *, #30400, .F. ) ;
#48002=ORIENTED_EDGE ( 'NONE', *, *, #105168, .T. ) ;
#48003=ORIENTED_EDGE ( 'NONE', *, *, #40249, .F. ) ;
#48005=ORIENTED_EDGE ( 'NONE', *, *, #47938, .T. ) ;
#48006=ORIENTED_EDGE ( 'NONE', *, *, #113497, .T. ) ;
#48007=VERTEX_POINT ( 'NONE', #124827 ) ;
#48010=ORIENTED_EDGE ( 'NONE', *, *, #102156, .T. ) ;
#48011=CARTESIAN_POINT ( 'NONE',  ( -6.134995737516187653, 3.759292476615678336, 15.36553568819727644 ) ) ;
#48013=VECTOR ( 'NONE', #20919, 1000.000000000000227 ) ;
#48014=DIRECTION ( 'NONE',  ( 0.7071067811865487940, 0.7071067811865463515, 0.000000000000000000 ) ) ;
#48016=EDGE_LOOP ( 'NONE', ( #25262, #6444, #88765, #137886 ) ) ;
#48018=CARTESIAN_POINT ( 'NONE',  ( 33.18398860626899705, 28.73617430169810305, 5.000000000000000000 ) ) ;
#48019=CARTESIAN_POINT ( 'NONE',  ( -14.52663903635775533, -5.240707523384225297, 16.25846745537492311 ) ) ;
#48021=VECTOR ( 'NONE', #139550, 1000.000000000000000 ) ;
#48022=LINE ( 'NONE', #46629, #104744 ) ;
#48023=DIRECTION ( 'NONE',  ( -0.000000000000000000, 0.3543493200069153248, 0.9351131265310292928 ) ) ;
#48025=FACE_OUTER_BOUND ( 'NONE', #24554, .T. ) ;
#48026=EDGE_CURVE ( 'NONE', #131139, #122126, #11753, .T. ) ;
#48027=VECTOR ( 'NONE', #739, 1000.000000000000227 ) ;
#48028=ORIENTED_EDGE ( 'NONE', *, *, #77901, .F. ) ;
#48029=ORIENTED_EDGE ( 'NONE', *, *, #38165, .T. ) ;
#48031=ORIENTED_EDGE ( 'NONE', *, *, #52187, .T. ) ;
#48032=ORIENTED_EDGE ( 'NONE', *, *, #125803, .T. ) ;
#48033=FACE_OUTER_BOUND ( 'NONE', #72296, .T. ) ;
#48034=AXIS2_PLACEMENT_3D ( 'NONE', #22151, #109896, #10558 ) ;
#48035=ORIENTED_EDGE ( 'NONE', *, *, #93401, .F. ) ;
#48036=LINE ( 'NONE', #15345, #43259 ) ;
#48037=FACE_OUTER_BOUND ( 'NONE', #49883, .T. ) ;
#48038=CARTESIAN_POINT ( 'NONE',  ( 2.510786437626908008, -27.52281430457053446, 5.000000000000000000 ) ) ;
#48040=VERTEX_POINT ( 'NONE', #58197 ) ;
#48042=EDGE_LOOP ( 'NONE', ( #40640, #78002, #4914, #30109 ) ) ;
#48044=LINE ( 'NONE', #136447, #63853 ) ;
#48046=ORIENTED_EDGE ( 'NONE', *, *, #76989, .T. ) ;
#48047=VERTEX_POINT ( 'NONE', #35723 ) ;
#48048=DIRECTION ( 'NONE',  ( -0.7071067811865486830, -0.7071067811865464625, 0.000000000000000000 ) ) ;
#48049=CARTESIAN_POINT ( 'NONE',  ( -9.489213562373095101, -27.52281430457062328, 5.000000000000000000 ) ) ;
#48050=DIRECTION ( 'NONE',  ( -0.7071067811865487940, 0.7071067811865463515, 0.000000000000000000 ) ) ;
#48051=AXIS2_PLACEMENT_3D ( 'NONE', #135828, #136520, #2420 ) ;
#48052=VECTOR ( 'NONE', #28878, 999.9999999999998863 ) ;
#48054=CARTESIAN_POINT ( 'NONE',  ( 0.000000000000000000, 0.000000000000000000, 5.000000000000000000 ) ) ;
#48055=LINE ( 'NONE', #13954, #66334 ) ;
#48056=ORIENTED_EDGE ( 'NONE', *, *, #7484, .T. ) ;
#48057=ORIENTED_EDGE ( 'NONE', *, *, #21131, .T. ) ;
#48058=VECTOR ( 'NONE', #102606, 999.9999999999998863 ) ;
#48059=LINE ( 'NONE', #36459, #72489 ) ;
#48060=VERTEX_POINT ( 'NONE', #56038 ) ;
#48061=DIRECTION ( 'NONE',  ( -0.3543493200069162685, -0.000000000000000000, -0.9351131265310288487 ) ) ;
#48062=VERTEX_POINT ( 'NONE', #124114 ) ;
#48063=CARTESIAN_POINT ( 'NONE',  ( 6.299744871391586898, -27.71228299555210484, 4.000000000000000000 ) ) ;
#48064=EDGE_CURVE ( 'NONE', #25081, #130179, #2292, .T. ) ;
#48066=FACE_BOUND ( 'NONE', #33204, .T. ) ;
#48067=CARTESIAN_POINT ( 'NONE',  ( -14.99999999999989519, -19.06887692260762179, 4.000000000000000000 ) ) ;
#48068=EDGE_CURVE ( 'NONE', #61017, #81835, #100229, .T. ) ;
#48069=EDGE_CURVE ( 'NONE', #50737, #110777, #79943, .T. ) ;
#48071=PLANE ( 'NONE',  #115048 ) ;
#48073=DIRECTION ( 'NONE',  ( 0.7071067811865486830, -0.7071067811865464625, -0.000000000000000000 ) ) ;
#48075=LINE ( 'NONE', #81438, #17033 ) ;
#48076=ORIENTED_EDGE ( 'NONE', *, *, #6960, .F. ) ;
#48077=ADVANCED_FACE ( 'NONE', ( #57455 ), #14643, .F. ) ;
#48078=EDGE_CURVE ( 'NONE', #44266, #20400, #91501, .T. ) ;
#48079=ORIENTED_EDGE ( 'NONE', *, *, #69380, .F. ) ;
#48082=EDGE_CURVE ( 'NONE', #7189, #19552, #24095, .T. ) ;
#48083=VECTOR ( 'NONE', #15914, 1000.000000000000227 ) ;
#48084=DIRECTION ( 'NONE',  ( -0.6830127018922180770, -0.6830127018922204085, -0.2588190451025213501 ) ) ;
#48085=EDGE_CURVE ( 'NONE', #55021, #59483, #1581, .T. ) ;
#48086=ORIENTED_EDGE ( 'NONE', *, *, #1693, .T. ) ;
#48087=EDGE_CURVE ( 'NONE', #50352, #63182, #122670, .T. ) ;
#48088=DIRECTION ( 'NONE',  ( -0.3543493200069162685, -0.000000000000000000, -0.9351131265310288487 ) ) ;
#48089=EDGE_CURVE ( 'NONE', #29579, #3561, #43857, .T. ) ;
#48090=CARTESIAN_POINT ( 'NONE',  ( -17.99999999999986855, 17.58746187583906462, 4.000000000000000000 ) ) ;
#48091=PLANE ( 'NONE',  #8782 ) ;
#48092=CARTESIAN_POINT ( 'NONE',  ( -25.99806943317883423, -22.22500000000000142, 4.500000000000000888 ) ) ;
#48093=CARTESIAN_POINT ( 'NONE',  ( 80.99451991528748351, 28.92564299267994699, 4.000000000000000000 ) ) ;
#48094=DIRECTION ( 'NONE',  ( -0.6830127018922180770, -0.6830127018922204085, -0.2588190451025213501 ) ) ;
#48095=EDGE_LOOP ( 'NONE', ( #100862, #87752, #5867, #110794 ) ) ;
#48096=EDGE_LOOP ( 'NONE', ( #93509, #111681, #77183, #14699 ) ) ;
#48098=AXIS2_PLACEMENT_3D ( 'NONE', #112293, #69513, #642 ) ;
#48099=CARTESIAN_POINT ( 'NONE',  ( -26.99999999999981171, -15.03360074219758147, 5.000000000000000000 ) ) ;
#48100=VERTEX_POINT ( 'NONE', #111822 ) ;
#48101=EDGE_CURVE ( 'NONE', #13228, #70912, #88650, .T. ) ;
#48104=ORIENTED_EDGE ( 'NONE', *, *, #18841, .T. ) ;
#48105=LINE ( 'NONE', #94435, #22994 ) ;
#48106=VERTEX_POINT ( 'NONE', #132881 ) ;
#48107=LINE ( 'NONE', #48824, #64822 ) ;
#48108=EDGE_CURVE ( 'NONE', #17123, #41182, #24366, .T. ) ;
#48109=AXIS2_PLACEMENT_3D ( 'NONE', #100676, #12920, #122400 ) ;
#48110=AXIS2_PLACEMENT_3D ( 'NONE', #55933, #89943, #1491 ) ;
#48113=DIRECTION ( 'NONE',  ( 0.6830127018922180770, -0.6830127018922204085, -0.2588190451025213501 ) ) ;
#48114=ORIENTED_EDGE ( 'NONE', *, *, #66607, .F. ) ;
#48115=LINE ( 'NONE', #82194, #1718 ) ;
#48117=CARTESIAN_POINT ( 'NONE',  ( -13.49999999999990230, -15.29013452822855612, 0.3645803511610036796 ) ) ;
#48118=CARTESIAN_POINT ( 'NONE',  ( -34.92500000000001137, -5.405284025385249436, -5.470147491473926316 ) ) ;
#48119=ORIENTED_EDGE ( 'NONE', *, *, #92219, .T. ) ;
#48120=EDGE_LOOP ( 'NONE', ( #66063, #35550, #65270, #87205, #103104 ) ) ;
#48122=CARTESIAN_POINT ( 'NONE',  ( 18.70710678118641468, -3.740707523384243505, 5.000000000000000000 ) ) ;
#48123=LINE ( 'NONE', #92305, #109557 ) ;
#48124=ORIENTED_EDGE ( 'NONE', *, *, #95616, .T. ) ;
#48125=EDGE_CURVE ( 'NONE', #43222, #135455, #13180, .T. ) ;
#48126=DIRECTION ( 'NONE',  ( -0.7071067811865486830, 0.7071067811865464625, 0.000000000000000000 ) ) ;
#48127=EDGE_CURVE ( 'NONE', #58607, #126947, #81354, .T. ) ;
#48128=DIRECTION ( 'NONE',  ( -0.000000000000000000, 0.3543493200069153248, 0.9351131265310292928 ) ) ;
#48130=CARTESIAN_POINT ( 'NONE',  ( -9.299744871391588674, -27.71228299555212971, 4.000000000000000000 ) ) ;
#48131=ORIENTED_EDGE ( 'NONE', *, *, #6424, .T. ) ;
#48132=DIRECTION ( 'NONE',  ( 0.7071067811865486830, -0.7071067811865464625, -0.000000000000000000 ) ) ;
#48133=CARTESIAN_POINT ( 'NONE',  ( -27.18398860626900060, 28.73617430169806042, 5.000000000000000000 ) ) ;
#48134=ADVANCED_FACE ( 'NONE', ( #128411 ), #29088, .T. ) ;
#48135=CARTESIAN_POINT ( 'NONE',  ( 6.792893218813414791, 3.759292476615680112, 5.000000000000000000 ) ) ;
#48137=PLANE ( 'NONE',  #124813 ) ;
#48138=ORIENTED_EDGE ( 'NONE', *, *, #90365, .F. ) ;
#48140=AXIS2_PLACEMENT_3D ( 'NONE', #3635, #49364, #27549 ) ;
#48141=DIRECTION ( 'NONE',  ( 0.7071067811865487940, 0.7071067811865463515, -0.000000000000000000 ) ) ;
#48142=DIRECTION ( 'NONE',  ( -0.000000000000000000, 0.000000000000000000, 1.000000000000000000 ) ) ;
#48145=DIRECTION ( 'NONE',  ( 1.000000000000000000, 0.000000000000000000, 0.000000000000000000 ) ) ;
#48146=LINE ( 'NONE', #92327, #69120 ) ;
#48147=CARTESIAN_POINT ( 'NONE',  ( 72.29974487139158157, -27.71228299555256669, 4.000000000000000000 ) ) ;
#48148=VERTEX_POINT ( 'NONE', #15317 ) ;
#48149=ADVANCED_FACE ( 'NONE', ( #105899 ), #38541, .F. ) ;
#48151=CARTESIAN_POINT ( 'NONE',  ( 14.99999999999989697, 19.55218569542897100, 5.000000000000000000 ) ) ;
#48154=CARTESIAN_POINT ( 'NONE',  ( -0.7933393645784717618, 21.75929247661549581, 4.998822639870701856 ) ) ;
#48155=CARTESIAN_POINT ( 'NONE',  ( 2.816011393730999401, 28.73617430169785436, 5.000000000000000000 ) ) ;
#48156=EDGE_CURVE ( 'NONE', #29361, #40495, #37847, .T. ) ;
#48157=ORIENTED_EDGE ( 'NONE', *, *, #122596, .F. ) ;
#48158=DIRECTION ( 'NONE',  ( 0.7071067811865487940, 0.7071067811865463515, -0.000000000000000000 ) ) ;
#48159=VERTEX_POINT ( 'NONE', #116802 ) ;
#48160=CARTESIAN_POINT ( 'NONE',  ( 13.82816939922342669, -11.24070752338417201, 4.000000000000000000 ) ) ;
#48162=DIRECTION ( 'NONE',  ( 0.7071067811865487940, 0.7071067811865463515, 0.000000000000000000 ) ) ;
#48163=PLANE ( 'NONE',  #55599 ) ;
#48164=EDGE_CURVE ( 'NONE', #85990, #91413, #83480, .T. ) ;
#48166=ORIENTED_EDGE ( 'NONE', *, *, #106727, .F. ) ;
#48167=EDGE_CURVE ( 'NONE', #42625, #1467, #18167, .T. ) ;
#48170=DIRECTION ( 'NONE',  ( -0.7071067811865487940, 0.7071067811865463515, 0.000000000000000000 ) ) ;
#48173=LINE ( 'NONE', #138039, #22818 ) ;
#48174=EDGE_LOOP ( 'NONE', ( #565, #93605, #35278, #128112 ) ) ;
#48175=EDGE_LOOP ( 'NONE', ( #54940, #27955, #73660, #92306 ) ) ;
#48178=DIRECTION ( 'NONE',  ( 0.6830127018922180770, -0.6830127018922204085, -0.2588190451025213501 ) ) ;
#48179=DIRECTION ( 'NONE',  ( 0.6830127018922180770, -0.6830127018922204085, -0.2588190451025213501 ) ) ;
#48182=EDGE_CURVE ( 'NONE', #50766, #130550, #48703, .T. ) ;
#48183=DIRECTION ( 'NONE',  ( -0.7071067811865487940, 0.7071067811865463515, 0.000000000000000000 ) ) ;
#48184=EDGE_CURVE ( 'NONE', #68957, #136293, #26240, .T. ) ;
#48187=CARTESIAN_POINT ( 'NONE',  ( 63.48921356237309510, -27.52281430457099631, 5.000000000000000000 ) ) ;
#48188=ORIENTED_EDGE ( 'NONE', *, *, #25478, .F. ) ;
#48190=CARTESIAN_POINT ( 'NONE',  ( -63.18398860626900415, 28.73617430169831621, 5.000000000000000000 ) ) ;
#48192=CARTESIAN_POINT ( 'NONE',  ( 27.71230993966009137, -21.73547319004781997, 4.999917730833664642 ) ) ;
#48193=CARTESIAN_POINT ( 'NONE',  ( -8.999999999999937828, 16.55218569542900298, 5.000000000000000000 ) ) ;
#48194=AXIS2_PLACEMENT_3D ( 'NONE', #126484, #49687, #83007 ) ;
#48195=LINE ( 'NONE', #81566, #34767 ) ;
#48196=EDGE_CURVE ( 'NONE', #54208, #36944, #116081, .T. ) ;
#48198=ORIENTED_EDGE ( 'NONE', *, *, #83284, .T. ) ;
#48199=CARTESIAN_POINT ( 'NONE',  ( 42.29974487139158157, -27.71228299555235708, 4.000000000000000000 ) ) ;
#48200=DIRECTION ( 'NONE',  ( 0.3543493200069162685, -0.000000000000000000, -0.9351131265310288487 ) ) ;
#48201=FACE_OUTER_BOUND ( 'NONE', #126833, .T. ) ;
#48202=VECTOR ( 'NONE', #122046, 1000.000000000000000 ) ;
#48203=DIRECTION ( 'NONE',  ( -0.7071067811865487940, 0.7071067811865463515, -0.000000000000000000 ) ) ;
#48204=VECTOR ( 'NONE', #143447, 1000.000000000000227 ) ;
#48205=VERTEX_POINT ( 'NONE', #82764 ) ;
#48206=EDGE_LOOP ( 'NONE', ( #31557, #63659, #29294, #80543 ) ) ;
#48207=DIRECTION ( 'NONE',  ( 0.7071067811865487940, 0.7071067811865463515, 0.000000000000000000 ) ) ;
#48208=DIRECTION ( 'NONE',  ( 0.7071067811865486830, -0.7071067811865464625, -0.000000000000000000 ) ) ;
#48209=CARTESIAN_POINT ( 'NONE',  ( -63.18398860626900415, 28.73617430169831621, 5.000000000000000000 ) ) ;
#48210=DIRECTION ( 'NONE',  ( -0.000000000000000000, 0.000000000000000000, 1.000000000000000000 ) ) ;
#48211=ORIENTED_EDGE ( 'NONE', *, *, #50407, .T. ) ;
#48212=ORIENTED_EDGE ( 'NONE', *, *, #110907, .T. ) ;
#48216=ORIENTED_EDGE ( 'NONE', *, *, #46428, .F. ) ;
#48217=DIRECTION ( 'NONE',  ( -0.3543493200069162685, -0.000000000000000000, -0.9351131265310288487 ) ) ;
#48218=DIRECTION ( 'NONE',  ( -0.000000000000000000, 0.000000000000000000, 1.000000000000000000 ) ) ;
#48219=VECTOR ( 'NONE', #3547, 1000.000000000000000 ) ;
#48220=VECTOR ( 'NONE', #99456, 1000.000000000000000 ) ;
#48221=FACE_BOUND ( 'NONE', #8629, .T. ) ;
#48222=FACE_OUTER_BOUND ( 'NONE', #45382, .T. ) ;
#48223=EDGE_CURVE ( 'NONE', #44804, #75865, #70504, .T. ) ;
#48225=PLANE ( 'NONE',  #108370 ) ;
#48226=PLANE ( 'NONE',  #103632 ) ;
#48229=VERTEX_POINT ( 'NONE', #82080 ) ;
#48230=EDGE_CURVE ( 'NONE', #19849, #69925, #39998, .T. ) ;
#48233=ORIENTED_EDGE ( 'NONE', *, *, #14444, .F. ) ;
#48234=EDGE_CURVE ( 'NONE', #20671, #141363, #26937, .T. ) ;
#48235=LINE ( 'NONE', #14886, #39636 ) ;
#48236=EDGE_CURVE ( 'NONE', #142768, #48818, #71185, .T. ) ;
#48237=LINE ( 'NONE', #39528, #5252 ) ;
#48238=EDGE_CURVE ( 'NONE', #65454, #35767, #16776, .T. ) ;
#48240=DIRECTION ( 'NONE',  ( 0.7071067811865487940, -0.7071067811865463515, 0.000000000000000000 ) ) ;
#48241=ORIENTED_EDGE ( 'NONE', *, *, #97815, .T. ) ;
#48247=DIRECTION ( 'NONE',  ( 0.3543493200069162685, -0.000000000000000000, -0.9351131265310288487 ) ) ;
#48248=PLANE ( 'NONE',  #71685 ) ;
#48251=CARTESIAN_POINT ( 'NONE',  ( -9.183988606268997046, 28.73617430169793607, 5.000000000000000000 ) ) ;
#48252=DIRECTION ( 'NONE',  ( 0.7071067811865486830, -0.7071067811865464625, -0.000000000000000000 ) ) ;
#48253=EDGE_CURVE ( 'NONE', #53545, #116521, #50843, .T. ) ;
#48254=ORIENTED_EDGE ( 'NONE', *, *, #131620, .T. ) ;
#48255=EDGE_LOOP ( 'NONE', ( #9455, #128469, #51490, #119752 ) ) ;
#48259=EDGE_LOOP ( 'NONE', ( #38663, #129742, #48233, #141291 ) ) ;
#48260=EDGE_CURVE ( 'NONE', #48333, #31876, #136407, .T. ) ;
#48263=ORIENTED_EDGE ( 'NONE', *, *, #140856, .F. ) ;
#48264=ORIENTED_EDGE ( 'NONE', *, *, #46508, .F. ) ;
#48265=LINE ( 'NONE', #92462, #62685 ) ;
#48266=CARTESIAN_POINT ( 'NONE',  ( 8.999999999999941380, -0.03360074219773377668, 5.000000000000000000 ) ) ;
#48267=CARTESIAN_POINT ( 'NONE',  ( 14.99999999999989164, -21.03360074219752462, 5.000000000000000000 ) ) ;
#48268=EDGE_LOOP ( 'NONE', ( #43852, #84823, #129479, #68072 ) ) ;
#48269=VERTEX_POINT ( 'NONE', #140012 ) ;
#48270=DIRECTION ( 'NONE',  ( 0.7071067811865487940, 0.7071067811865463515, 0.000000000000000000 ) ) ;
#48271=DIRECTION ( 'NONE',  ( -0.7071067811865486830, 0.7071067811865464625, 0.000000000000000000 ) ) ;
#48274=CARTESIAN_POINT ( 'NONE',  ( 39.48921356237310221, -27.52281430457082934, 5.000000000000000000 ) ) ;
#48275=ORIENTED_EDGE ( 'NONE', *, *, #15741, .T. ) ;
#48276=ORIENTED_EDGE ( 'NONE', *, *, #2710, .F. ) ;
#48277=EDGE_LOOP ( 'NONE', ( #64621, #48166, #112689, #51561 ) ) ;
#48278=VERTEX_POINT ( 'NONE', #10176 ) ;
#48280=CARTESIAN_POINT ( 'NONE',  ( -1.265066702820505373, 12.75929247661558996, 18.34774599283956675 ) ) ;
#48281=VECTOR ( 'NONE', #20771, 1000.000000000000000 ) ;
#48282=VECTOR ( 'NONE', #28150, 999.9999999999998863 ) ;
#48284=DIRECTION ( 'NONE',  ( 0.7071067811865487940, 0.7071067811865463515, 0.000000000000000000 ) ) ;
#48285=VECTOR ( 'NONE', #120034, 1000.000000000000227 ) ;
#48286=DIRECTION ( 'NONE',  ( 1.000000000000000000, 0.000000000000000000, 0.000000000000000000 ) ) ;
#48287=CARTESIAN_POINT ( 'NONE',  ( -2.999999999999983569, 19.93112307739198386, 4.000000000000000000 ) ) ;
#48288=VECTOR ( 'NONE', #122274, 999.9999999999998863 ) ;
#48289=PLANE ( 'NONE',  #37281 ) ;
#48290=ORIENTED_EDGE ( 'NONE', *, *, #103119, .F. ) ;
#48291=AXIS2_PLACEMENT_3D ( 'NONE', #81559, #38041, #91001 ) ;
#48292=DIRECTION ( 'NONE',  ( -0.3543493200069162685, -0.000000000000000000, -0.9351131265310288487 ) ) ;
#48295=CARTESIAN_POINT ( 'NONE',  ( 8.483345613589499123, 22.22500000000000142, 4.500000000000000888 ) ) ;
#48296=PLANE ( 'NONE',  #39081 ) ;
#48297=CARTESIAN_POINT ( 'NONE',  ( -5.287690060339683917, -21.73547319004781642, 4.999917730833664642 ) ) ;
#48298=ORIENTED_EDGE ( 'NONE', *, *, #94078, .T. ) ;
#48299=ORIENTED_EDGE ( 'NONE', *, *, #64623, .F. ) ;
#48300=ADVANCED_FACE ( 'NONE', ( #53716 ), #97918, .F. ) ;
#48301=ORIENTED_EDGE ( 'NONE', *, *, #34068, .T. ) ;
#48302=DIRECTION ( 'NONE',  ( -8.817971600062199903E-18, 0.3543493200069153248, 0.9351131265310292928 ) ) ;
#48303=PLANE ( 'NONE',  #81215 ) ;
#48304=LINE ( 'NONE', #72255, #91638 ) ;
#48306=DIRECTION ( 'NONE',  ( 0.7071067811865486830, -0.7071067811865464625, -0.000000000000000000 ) ) ;
#48307=CARTESIAN_POINT ( 'NONE',  ( 34.47516574401890210, -11.97193265888406088, 4.998110765256833510 ) ) ;
#48308=CARTESIAN_POINT ( 'NONE',  ( 15.18398860626900237, 28.73617430169797871, 5.000000000000000000 ) ) ;
#48312=LINE ( 'NONE', #38869, #90012 ) ;
#48313=DIRECTION ( 'NONE',  ( -0.6830127018922181881, 0.6830127018922202975, -0.2588190451025214056 ) ) ;
#48315=CARTESIAN_POINT ( 'NONE',  ( 29.99999999999978328, 14.58746187583910192, 4.000000000000000000 ) ) ;
#48316=CARTESIAN_POINT ( 'NONE',  ( -25.43312800248726546, -21.74070752338406365, 6.915939825044133293 ) ) ;
#48317=EDGE_LOOP ( 'NONE', ( #69182, #138516, #73634, #135546 ) ) ;
#48318=VECTOR ( 'NONE', #61043, 1000.000000000000000 ) ;
#48319=FACE_OUTER_BOUND ( 'NONE', #41700, .T. ) ;
#48320=EDGE_LOOP ( 'NONE', ( #102414, #54137, #82266, #134027 ) ) ;
#48321=VECTOR ( 'NONE', #81382, 999.9999999999998863 ) ;
#48322=( BOUNDED_CURVE ( )  B_SPLINE_CURVE ( 3, ( #102458, #47394, #137216, #70564 ),
 .UNSPECIFIED., .F., .T. ) 
 B_SPLINE_CURVE_WITH_KNOTS ( ( 4, 4 ),
 ( 2.356194490192346613, 2.506762762968526292 ),
 .UNSPECIFIED. ) 
 CURVE ( )  GEOMETRIC_REPRESENTATION_ITEM ( )  RATIONAL_B_SPLINE_CURVE ( ( 1.000000000000000000, 0.9981116584018958626, 0.9981116584018958626, 1.000000000000000000 ) ) 
 REPRESENTATION_ITEM ( '' )  );
#48323=VECTOR ( 'NONE', #133554, 999.9999999999998863 ) ;
#48325=DIRECTION ( 'NONE',  ( 0.7071067811865486830, -0.7071067811865464625, -0.000000000000000000 ) ) ;
#48326=CARTESIAN_POINT ( 'NONE',  ( 2.524873872149526743, 14.25929247661556865, 9.797011795316644012 ) ) ;
#48327=ORIENTED_EDGE ( 'NONE', *, *, #34704, .T. ) ;
#48328=EDGE_CURVE ( 'NONE', #1167, #35612, #25209, .T. ) ;
#48329=LINE ( 'NONE', #125902, #2373 ) ;
#48330=DIRECTION ( 'NONE',  ( -0.7071067811865486830, -0.7071067811865464625, 0.000000000000000000 ) ) ;
#48331=EDGE_LOOP ( 'NONE', ( #95554, #43989, #30234, #6172 ) ) ;
#48332=LINE ( 'NONE', #46959, #60126 ) ;
#48333=VERTEX_POINT ( 'NONE', #19632 ) ;
#48334=LINE ( 'NONE', #104106, #125483 ) ;
#48335=ORIENTED_EDGE ( 'NONE', *, *, #92942, .T. ) ;
#48337=CARTESIAN_POINT ( 'NONE',  ( -16.83455439249994612, 8.717631302929021331, 5.000000000000000000 ) ) ;
#48339=CARTESIAN_POINT ( 'NONE',  ( -13.17183060077637613, -20.24070752338407075, 4.000000000000000000 ) ) ;
#48342=LINE ( 'NONE', #115692, #19151 ) ;
#48343=CARTESIAN_POINT ( 'NONE',  ( -42.48921356237308800, -27.52281430457085065, 5.000000000000000000 ) ) ;
#48344=LINE ( 'NONE', #83120, #97023 ) ;
#48346=CARTESIAN_POINT ( 'NONE',  ( -42.29974487139158157, -27.71228299555235708, 4.000000000000000000 ) ) ;
#48347=VECTOR ( 'NONE', #81667, 1000.000000000000000 ) ;
#48349=ORIENTED_EDGE ( 'NONE', *, *, #14738, .T. ) ;
#48350=LINE ( 'NONE', #2682, #39709 ) ;
#48351=ORIENTED_EDGE ( 'NONE', *, *, #26511, .F. ) ;
#48352=EDGE_CURVE ( 'NONE', #89986, #28308, #63876, .T. ) ;
#48354=DIRECTION ( 'NONE',  ( 0.3543493200069162685, -0.000000000000000000, -0.9351131265310288487 ) ) ;
#48356=CARTESIAN_POINT ( 'NONE',  ( 34.92499999999998295, 4.512461875839424152, 4.000000000000000000 ) ) ;
#48357=VERTEX_POINT ( 'NONE', #21048 ) ;
#48358=CARTESIAN_POINT ( 'NONE',  ( 7.149738618221213038, -22.22500000000000142, -10.94369129876685420 ) ) ;
#48360=ORIENTED_EDGE ( 'NONE', *, *, #104721, .F. ) ;
#48361=DIRECTION ( 'NONE',  ( -0.3543493200069163240, 4.681814790819596721E-17, -0.9351131265310288487 ) ) ;
#48362=EDGE_CURVE ( 'NONE', #59299, #23063, #8702, .T. ) ;
#48363=CARTESIAN_POINT ( 'NONE',  ( -23.67183060077630685, -21.74070752338406720, 4.000000000000000000 ) ) ;
#48365=ORIENTED_EDGE ( 'NONE', *, *, #49969, .T. ) ;
#48366=LINE ( 'NONE', #136799, #85345 ) ;
#48367=FACE_OUTER_BOUND ( 'NONE', #60303, .T. ) ;
#48369=VERTEX_POINT ( 'NONE', #52953 ) ;
#48371=VERTEX_POINT ( 'NONE', #119630 ) ;
#48373=ORIENTED_EDGE ( 'NONE', *, *, #21484, .F. ) ;
#48374=DIRECTION ( 'NONE',  ( -0.7071067811865486830, 0.7071067811865464625, 0.000000000000000000 ) ) ;
#48375=CARTESIAN_POINT ( 'NONE',  ( 17.99999999999987921, -6.412538124160682251, 4.000000000000000000 ) ) ;
#48376=CARTESIAN_POINT ( 'NONE',  ( -21.64790440752752687, 22.22500000000000142, 10.03118784388419016 ) ) ;
#48377=LINE ( 'NONE', #78897, #140395 ) ;
#48378=ORIENTED_EDGE ( 'NONE', *, *, #1887, .T. ) ;
#48380=FACE_OUTER_BOUND ( 'NONE', #34130, .T. ) ;
#48381=DIRECTION ( 'NONE',  ( -0.7071067811865487940, 0.7071067811865463515, -0.000000000000000000 ) ) ;
#48383=ORIENTED_EDGE ( 'NONE', *, *, #89719, .F. ) ;
#48384=DIRECTION ( 'NONE',  ( -0.7071067811865486830, -0.7071067811865464625, -0.000000000000000000 ) ) ;
#48385=FACE_OUTER_BOUND ( 'NONE', #62086, .T. ) ;
#48386=LINE ( 'NONE', #125966, #121081 ) ;
#48387=AXIS2_PLACEMENT_3D ( 'NONE', #29332, #51831, #40943 ) ;
#48388=VECTOR ( 'NONE', #65079, 999.9999999999998863 ) ;
#48389=ORIENTED_EDGE ( 'NONE', *, *, #48464, .F. ) ;
#48391=DIRECTION ( 'NONE',  ( -0.7071067811865486830, 0.7071067811865464625, 0.000000000000000000 ) ) ;
#48396=DIRECTION ( 'NONE',  ( -0.3543493200069162685, -0.000000000000000000, -0.9351131265310288487 ) ) ;
#48399=ADVANCED_FACE ( 'NONE', ( #8020 ), #98614, .F. ) ;
#48400=VERTEX_POINT ( 'NONE', #86339 ) ;
#48401=VERTEX_POINT ( 'NONE', #63180 ) ;
#48402=ADVANCED_FACE ( 'NONE', ( #121080 ), #107353, .F. ) ;
#48407=ADVANCED_FACE ( 'NONE', ( #96442 ), #142156, .T. ) ;
#48409=VECTOR ( 'NONE', #37865, 1000.000000000000000 ) ;
#48410=FACE_OUTER_BOUND ( 'NONE', #134784, .T. ) ;
#48411=ORIENTED_EDGE ( 'NONE', *, *, #36069, .F. ) ;
#48412=DIRECTION ( 'NONE',  ( 0.7071067811865487940, 0.7071067811865463515, 0.000000000000000000 ) ) ;
#48413=CARTESIAN_POINT ( 'NONE',  ( 1.499999999999990896, -15.29013452822854546, 0.3645803511610392622 ) ) ;
#48414=CARTESIAN_POINT ( 'NONE',  ( 31.49999999999978684, 1.087461875839228931, 4.000000000000000000 ) ) ;
#48415=AXIS2_PLACEMENT_3D ( 'NONE', #46084, #6071, #59804 ) ;
#48416=FACE_OUTER_BOUND ( 'NONE', #64412, .T. ) ;
#48417=ORIENTED_EDGE ( 'NONE', *, *, #37689, .T. ) ;
#48418=VECTOR ( 'NONE', #17125, 1000.000000000000227 ) ;
#48419=CARTESIAN_POINT ( 'NONE',  ( 60.48921356237309510, -27.52281430457097500, 5.000000000000000000 ) ) ;
#48421=VECTOR ( 'NONE', #36035, 999.9999999999998863 ) ;
#48422=EDGE_CURVE ( 'NONE', #139534, #134437, #20763, .T. ) ;
#48424=PLANE ( 'NONE',  #22598 ) ;
#48426=EDGE_CURVE ( 'NONE', #61464, #131664, #110894, .T. ) ;
#48427=VERTEX_POINT ( 'NONE', #36238 ) ;
#48428=CARTESIAN_POINT ( 'NONE',  ( 8.207106781186485733, 15.75929247661555976, 5.000000000000000000 ) ) ;
#48429=VERTEX_POINT ( 'NONE', #78311 ) ;
#48430=ORIENTED_EDGE ( 'NONE', *, *, #102207, .F. ) ;
#48433=ORIENTED_EDGE ( 'NONE', *, *, #1606, .T. ) ;
#48436=LINE ( 'NONE', #112971, #85865 ) ;
#48437=LINE ( 'NONE', #81085, #102766 ) ;
#48439=CARTESIAN_POINT ( 'NONE',  ( -4.499999999999962697, -5.568876922607757685, 4.000000000000000000 ) ) ;
#48443=ADVANCED_FACE ( 'NONE', ( #79783 ), #47165, .F. ) ;
#48444=CARTESIAN_POINT ( 'NONE',  ( 28.17183060077627133, -14.24070752338414003, 4.000000000000000000 ) ) ;
#48445=CARTESIAN_POINT ( 'NONE',  ( 34.92499999999998295, 1.077975372831902590, 13.01339814852642540 ) ) ;
#48447=EDGE_LOOP ( 'NONE', ( #83343, #711, #31533, #93510 ) ) ;
#48448=CARTESIAN_POINT ( 'NONE',  ( 3.299744871391591339, -27.71228299555208352, 4.000000000000000000 ) ) ;
#48449=CARTESIAN_POINT ( 'NONE',  ( 50.99451991528749062, 28.92564299267973738, 4.000000000000000000 ) ) ;
#48450=VERTEX_POINT ( 'NONE', #1420 ) ;
#48451=ORIENTED_EDGE ( 'NONE', *, *, #119882, .T. ) ;
#48452=ADVANCED_FACE ( 'NONE', ( #123260 ), #11579, .F. ) ;
#48453=CARTESIAN_POINT ( 'NONE',  ( -8.999999999999936051, 15.45873954670184780, -0.03131636524291922519 ) ) ;
#48454=VERTEX_POINT ( 'NONE', #88482 ) ;
#48455=PLANE ( 'NONE',  #83840 ) ;
#48456=LINE ( 'NONE', #93388, #8450 ) ;
#48457=DIRECTION ( 'NONE',  ( 0.7071067811865487940, 0.7071067811865463515, 0.000000000000000000 ) ) ;
#48458=DIRECTION ( 'NONE',  ( 0.7071067811865487940, 0.7071067811865463515, -0.000000000000000000 ) ) ;
#48459=ORIENTED_EDGE ( 'NONE', *, *, #106433, .F. ) ;
#48460=ADVANCED_FACE ( 'NONE', ( #123964 ), #46433, .F. ) ;
#48461=FACE_OUTER_BOUND ( 'NONE', #107837, .T. ) ;
#48462=EDGE_LOOP ( 'NONE', ( #17132, #114644, #20490, #114127 ) ) ;
#48463=CARTESIAN_POINT ( 'NONE',  ( -22.42819999999999681, 3.174999999999997602, 0.000000000000000000 ) ) ;
#48464=EDGE_CURVE ( 'NONE', #12209, #76457, #134859, .T. ) ;
#48466=CARTESIAN_POINT ( 'NONE',  ( 0.2997448713915885632, -27.71228299555206220, 4.000000000000000000 ) ) ;
#48468=ORIENTED_EDGE ( 'NONE', *, *, #16648, .F. ) ;
#48469=ORIENTED_EDGE ( 'NONE', *, *, #67119, .T. ) ;
#48470=VERTEX_POINT ( 'NONE', #100065 ) ;
#48471=DIRECTION ( 'NONE',  ( 0.3543493200069162685, -0.000000000000000000, -0.9351131265310288487 ) ) ;
#48472=CARTESIAN_POINT ( 'NONE',  ( -5.999999999999953815, -21.84840872380825161, 2.849755605029594019 ) ) ;
#48473=FACE_OUTER_BOUND ( 'NONE', #38644, .T. ) ;
#48474=DIRECTION ( 'NONE',  ( 0.7071067811865487940, -0.7071067811865463515, 0.000000000000000000 ) ) ;
#48475=ORIENTED_EDGE ( 'NONE', *, *, #32023, .F. ) ;
#48476=CARTESIAN_POINT ( 'NONE',  ( -22.82900182742193351, 7.795401085224272109, 5.000000000000000000 ) ) ;
#48478=CARTESIAN_POINT ( 'NONE',  ( -2.999999999999981792, -12.41253812416062985, 4.000000000000000000 ) ) ;
#48479=EDGE_CURVE ( 'NONE', #135356, #142320, #91345, .T. ) ;
#48480=LINE ( 'NONE', #68840, #25710 ) ;
#48481=LINE ( 'NONE', #81869, #127611 ) ;
#48482=EDGE_LOOP ( 'NONE', ( #40801, #38961 ) ) ;
#48483=CARTESIAN_POINT ( 'NONE',  ( 23.99451991528749062, 28.92564299267954908, 4.000000000000000000 ) ) ;
#48484=AXIS2_PLACEMENT_3D ( 'NONE', #136512, #72755, #83600 ) ;
#48485=AXIS2_PLACEMENT_3D ( 'NONE', #74526, #66497, #98404 ) ;
#48486=VECTOR ( 'NONE', #90097, 1000.000000000000000 ) ;
#48489=VECTOR ( 'NONE', #62164, 1000.000000000000000 ) ;
#48490=DIRECTION ( 'NONE',  ( -0.7071067811865486830, 0.7071067811865464625, 0.000000000000000000 ) ) ;
#48491=DIRECTION ( 'NONE',  ( -0.000000000000000000, -0.000000000000000000, 1.000000000000000000 ) ) ;
#48492=ORIENTED_EDGE ( 'NONE', *, *, #21131, .F. ) ;
#48494=ADVANCED_FACE ( 'NONE', ( #715 ), #134123, .T. ) ;
#48495=DIRECTION ( 'NONE',  ( 0.000000000000000000, 0.000000000000000000, 1.000000000000000000 ) ) ;
#48496=CARTESIAN_POINT ( 'NONE',  ( -11.99999999999991651, 4.965500833774314948, -4.007596771432631044 ) ) ;
#48497=DIRECTION ( 'NONE',  ( -0.7071067811865486830, 0.7071067811865464625, 0.000000000000000000 ) ) ;
#48500=AXIS2_PLACEMENT_3D ( 'NONE', #45686, #123945, #121761 ) ;
#48501=ORIENTED_EDGE ( 'NONE', *, *, #25668, .T. ) ;
#48502=LINE ( 'NONE', #92704, #10401 ) ;
#48503=DIRECTION ( 'NONE',  ( -0.000000000000000000, -0.3543493200069152693, 0.9351131265310292928 ) ) ;
#48505=LINE ( 'NONE', #50645, #136457 ) ;
#48508=DIRECTION ( 'NONE',  ( 0.7071067811865486830, -0.7071067811865464625, -0.000000000000000000 ) ) ;
#48510=CARTESIAN_POINT ( 'NONE',  ( -22.17183060077631396, -5.240707523384232402, 4.000000000000000000 ) ) ;
#48513=VECTOR ( 'NONE', #140168, 1000.000000000000000 ) ;
#48514=LINE ( 'NONE', #62259, #36719 ) ;
#48515=VECTOR ( 'NONE', #90186, 1000.000000000000000 ) ;
#48516=LINE ( 'NONE', #126091, #42013 ) ;
#48517=DIRECTION ( 'NONE',  ( -0.000000000000000000, 0.3543493200069153248, 0.9351131265310292928 ) ) ;
#48518=VERTEX_POINT ( 'NONE', #2867 ) ;
#48519=ORIENTED_EDGE ( 'NONE', *, *, #126966, .T. ) ;
#48521=VECTOR ( 'NONE', #48361, 1000.000000000000227 ) ;
#48522=ORIENTED_EDGE ( 'NONE', *, *, #120441, .F. ) ;
#48523=ORIENTED_EDGE ( 'NONE', *, *, #118015, .F. ) ;
#48524=EDGE_CURVE ( 'NONE', #10002, #86852, #34810, .T. ) ;
#48528=VERTEX_POINT ( 'NONE', #110194 ) ;
#48530=CARTESIAN_POINT ( 'NONE',  ( -30.09843580608217550, 11.25929247661560595, 10.79108189686400010 ) ) ;
#48531=VECTOR ( 'NONE', #57457, 1000.000000000000227 ) ;
#48533=VECTOR ( 'NONE', #119955, 1000.000000000000000 ) ;
#48534=CARTESIAN_POINT ( 'NONE',  ( 23.99999999999983302, -18.03360074219755660, 5.000000000000000000 ) ) ;
#48537=AXIS2_PLACEMENT_3D ( 'NONE', #18957, #94367, #44305 ) ;
#48538=EDGE_CURVE ( 'NONE', #98566, #18405, #143552, .T. ) ;
#48539=CARTESIAN_POINT ( 'NONE',  ( 5.229957205422025801, 21.73644205237997795, 5.000000000000000888 ) ) ;
#48540=CARTESIAN_POINT ( 'NONE',  ( 34.92499999999998295, -2.038703271653913962, -4.194424194487909929 ) ) ;
#48541=CARTESIAN_POINT ( 'NONE',  ( 0.000000000000000000, 0.000000000000000000, 5.000000000000000000 ) ) ;
#48542=VECTOR ( 'NONE', #89535, 999.9999999999998863 ) ;
#48543=CARTESIAN_POINT ( 'NONE',  ( 34.92499999999998295, 22.22500000000000142, 4.000000000000000000 ) ) ;
#48544=CARTESIAN_POINT ( 'NONE',  ( 15.72281430457048934, -21.72500000000000497, 5.000000000000000000 ) ) ;
#48545=CARTESIAN_POINT ( 'NONE',  ( 9.489213562373095101, -27.52281430457062328, 5.000000000000000000 ) ) ;
#48546=LINE ( 'NONE', #14487, #52239 ) ;
#48548=ORIENTED_EDGE ( 'NONE', *, *, #27709, .F. ) ;
#48549=ORIENTED_EDGE ( 'NONE', *, *, #30927, .T. ) ;
#48551=ADVANCED_FACE ( 'NONE', ( #89188 ), #133413, .F. ) ;
#48552=ORIENTED_EDGE ( 'NONE', *, *, #29580, .T. ) ;
#48553=EDGE_CURVE ( 'NONE', #66785, #32778, #67454, .T. ) ;
#48554=DIRECTION ( 'NONE',  ( -0.7071067811865486830, -0.7071067811865464625, 0.000000000000000000 ) ) ;
#48555=VECTOR ( 'NONE', #47143, 999.9999999999998863 ) ;
#48558=EDGE_CURVE ( 'NONE', #18419, #31469, #60138, .T. ) ;
#48559=DIRECTION ( 'NONE',  ( 0.7071067811865486830, 0.7071067811865463515, 0.000000000000000000 ) ) ;
#48562=ORIENTED_EDGE ( 'NONE', *, *, #23009, .F. ) ;
#48564=FACE_OUTER_BOUND ( 'NONE', #7612, .T. ) ;
#48565=DIRECTION ( 'NONE',  ( 0.3543493200069162685, -0.000000000000000000, -0.9351131265310288487 ) ) ;
#48566=LINE ( 'NONE', #69370, #66338 ) ;
#48567=EDGE_LOOP ( 'NONE', ( #1925, #56712, #48079, #89821 ) ) ;
#48572=ADVANCED_FACE ( 'NONE', ( #27460 ), #94856, .F. ) ;
#48574=EDGE_CURVE ( 'NONE', #11869, #135832, #126779, .T. ) ;
#48576=ORIENTED_EDGE ( 'NONE', *, *, #91613, .F. ) ;
#48577=VERTEX_POINT ( 'NONE', #82584 ) ;
#48578=EDGE_CURVE ( 'NONE', #15499, #7366, #14472, .T. ) ;
#48579=LINE ( 'NONE', #14519, #121964 ) ;
#48580=ORIENTED_EDGE ( 'NONE', *, *, #104007, .T. ) ;
#48581=ORIENTED_EDGE ( 'NONE', *, *, #19671, .T. ) ;
#48582=EDGE_CURVE ( 'NONE', #95370, #56470, #137696, .T. ) ;
#48584=FACE_OUTER_BOUND ( 'NONE', #139394, .T. ) ;
#48585=DIRECTION ( 'NONE',  ( 0.7071067811865487940, 0.7071067811865463515, 0.000000000000000000 ) ) ;
#48586=VERTEX_POINT ( 'NONE', #104304 ) ;
#48587=CARTESIAN_POINT ( 'NONE',  ( 15.83652871126539630, 15.75929247661555443, 9.299976744542956197 ) ) ;
#48588=AXIS2_PLACEMENT_3D ( 'NONE', #89392, #20541, #132935 ) ;
#48593=CARTESIAN_POINT ( 'NONE',  ( 32.29289321881323360, 5.259292476615672562, 5.000000000000000000 ) ) ;
#48594=VECTOR ( 'NONE', #77175, 1000.000000000000227 ) ;
#48595=DIRECTION ( 'NONE',  ( -0.7071067811865486830, -0.7071067811865464625, 0.000000000000000000 ) ) ;
#48596=FACE_BOUND ( 'NONE', #62968, .T. ) ;
#48597=EDGE_CURVE ( 'NONE', #91814, #10831, #39823, .T. ) ;
#48598=ORIENTED_EDGE ( 'NONE', *, *, #41251, .T. ) ;
#48599=CARTESIAN_POINT ( 'NONE',  ( 54.18398860626899705, 28.73617430169825226, 5.000000000000000000 ) ) ;
#48601=CARTESIAN_POINT ( 'NONE',  ( 8.999999999999937828, -1.068876922607798985, 4.000000000000000000 ) ) ;
#48602=EDGE_CURVE ( 'NONE', #87366, #128057, #103595, .T. ) ;
#48603=ORIENTED_EDGE ( 'NONE', *, *, #79518, .F. ) ;
#48604=DIRECTION ( 'NONE',  ( -0.7071067811865487940, 0.7071067811865463515, 0.000000000000000000 ) ) ;
#48605=ORIENTED_EDGE ( 'NONE', *, *, #120053, .T. ) ;
#48606=ORIENTED_EDGE ( 'NONE', *, *, #133674, .F. ) ;
#48610=ORIENTED_EDGE ( 'NONE', *, *, #108588, .F. ) ;
#48611=EDGE_CURVE ( 'NONE', #84395, #80606, #71018, .T. ) ;
#48612=DIRECTION ( 'NONE',  ( -0.000000000000000000, -0.000000000000000000, 1.000000000000000000 ) ) ;
#48613=LINE ( 'NONE', #137046, #143275 ) ;
#48614=DIRECTION ( 'NONE',  ( -0.7071067811865487940, 0.7071067811865463515, 0.000000000000000000 ) ) ;
#48615=EDGE_LOOP ( 'NONE', ( #21037, #137139, #15225, #28020 ) ) ;
#48616=CARTESIAN_POINT ( 'NONE',  ( 19.77149322861323455, 20.25929247661551003, 7.808871592221815483 ) ) ;
#48617=PLANE ( 'NONE',  #122196 ) ;
#48618=AXIS2_PLACEMENT_3D ( 'NONE', #44448, #43698, #130734 ) ;
#48619=EDGE_CURVE ( 'NONE', #22222, #4418, #69598, .T. ) ;
#48621=VECTOR ( 'NONE', #22830, 1000.000000000000000 ) ;
#48622=CARTESIAN_POINT ( 'NONE',  ( -34.92500000000001137, -8.993876922607963564, 4.000000000000000000 ) ) ;
#48623=DIRECTION ( 'NONE',  ( 0.6830127018922180770, -0.6830127018922204085, -0.2588190451025213501 ) ) ;
#48624=CARTESIAN_POINT ( 'NONE',  ( -59.99451991528749772, 28.92564299267980132, 4.000000000000000000 ) ) ;
#48625=CARTESIAN_POINT ( 'NONE',  ( 0.000000000000000000, 0.000000000000000000, 5.000000000000000000 ) ) ;
#48626=ORIENTED_EDGE ( 'NONE', *, *, #68513, .T. ) ;
#48627=EDGE_LOOP ( 'NONE', ( #71342, #54399, #76871, #27204 ) ) ;
#48628=EDGE_CURVE ( 'NONE', #121707, #139204, #5705, .T. ) ;
#48630=ORIENTED_EDGE ( 'NONE', *, *, #101202, .T. ) ;
#48631=CARTESIAN_POINT ( 'NONE',  ( 1.499999999999980460, -12.08601207473289740, -10.46905243149095099 ) ) ;
#48633=VECTOR ( 'NONE', #718, 1000.000000000000000 ) ;
#48634=EDGE_LOOP ( 'NONE', ( #88561, #12520, #122921, #20553 ) ) ;
#48635=CARTESIAN_POINT ( 'NONE',  ( 10.17183060077640810, -5.240707523384230626, 4.000000000000000000 ) ) ;
#48636=CARTESIAN_POINT ( 'NONE',  ( 78.18398860626899705, 28.73617430169841924, 5.000000000000000000 ) ) ;
#48637=VECTOR ( 'NONE', #70425, 999.9999999999998863 ) ;
#48638=LINE ( 'NONE', #115264, #143471 ) ;
#48639=ORIENTED_EDGE ( 'NONE', *, *, #37793, .F. ) ;
#48640=VECTOR ( 'NONE', #126616, 1000.000000000000000 ) ;
#48641=EDGE_CURVE ( 'NONE', #5100, #113749, #94154, .T. ) ;
#48643=ORIENTED_EDGE ( 'NONE', *, *, #74583, .T. ) ;
#48644=CARTESIAN_POINT ( 'NONE',  ( 25.99806943317883068, -22.22500000000000142, 4.500000000000000888 ) ) ;
#48645=EDGE_CURVE ( 'NONE', #22290, #132198, #138390, .T. ) ;
#48647=AXIS2_PLACEMENT_3D ( 'NONE', #66970, #89421, #233 ) ;
#48649=VERTEX_POINT ( 'NONE', #72466 ) ;
#48652=DIRECTION ( 'NONE',  ( 0.3543493200069162685, -0.000000000000000000, -0.9351131265310288487 ) ) ;
#48653=ORIENTED_EDGE ( 'NONE', *, *, #10640, .F. ) ;
#48654=ORIENTED_EDGE ( 'NONE', *, *, #34468, .F. ) ;
#48655=LINE ( 'NONE', #37794, #7823 ) ;
#48659=DIRECTION ( 'NONE',  ( -0.7071067811865486830, -0.7071067811865464625, 0.000000000000000000 ) ) ;
#48661=EDGE_CURVE ( 'NONE', #75984, #70943, #127510, .T. ) ;
#48662=DIRECTION ( 'NONE',  ( 1.000000000000000000, 0.000000000000000000, 0.000000000000000000 ) ) ;
#48664=EDGE_LOOP ( 'NONE', ( #84180, #98132, #117533, #15746 ) ) ;
#48665=PLANE ( 'NONE',  #59990 ) ;
#48666=DIRECTION ( 'NONE',  ( -1.000000000000000000, -8.718663809566799855E-16, 0.000000000000000000 ) ) ;
#48669=SPHERICAL_SURFACE ( 'NONE', #58237, 0.5000000000000000000 ) ;
#48670=VECTOR ( 'NONE', #87857, 1000.000000000000000 ) ;
#48672=EDGE_LOOP ( 'NONE', ( #64887, #114217, #115850, #66502 ) ) ;
#48673=LINE ( 'NONE', #3688, #99581 ) ;
#48674=ORIENTED_EDGE ( 'NONE', *, *, #106291, .F. ) ;
#48676=LINE ( 'NONE', #104462, #105107 ) ;
#48677=CARTESIAN_POINT ( 'NONE',  ( -23.99999999999982592, 8.966399257802171618, 5.000000000000000000 ) ) ;
#48679=ORIENTED_EDGE ( 'NONE', *, *, #77611, .T. ) ;
#48682=DIRECTION ( 'NONE',  ( 0.6830127018922181881, 0.6830127018922202975, -0.2588190451025214056 ) ) ;
#48683=ORIENTED_EDGE ( 'NONE', *, *, #113914, .T. ) ;
#48685=PLANE ( 'NONE',  #62834 ) ;
#48686=EDGE_CURVE ( 'NONE', #26613, #19532, #92726, .T. ) ;
#48688=FACE_OUTER_BOUND ( 'NONE', #84844, .T. ) ;
#48690=CARTESIAN_POINT ( 'NONE',  ( -8.292893218813398803, 11.25929247661560062, 5.000000000000000000 ) ) ;
#48692=CARTESIAN_POINT ( 'NONE',  ( 34.92499999999998295, -8.143876922607498514, 4.000000000000000000 ) ) ;
#48693=VERTEX_POINT ( 'NONE', #26069 ) ;
#48694=EDGE_LOOP ( 'NONE', ( #129640, #31374, #3134, #24622 ) ) ;
#48695=VERTEX_POINT ( 'NONE', #70331 ) ;
#48696=VECTOR ( 'NONE', #38953, 999.9999999999998863 ) ;
#48698=VECTOR ( 'NONE', #36011, 1000.000000000000000 ) ;
#48699=VERTEX_POINT ( 'NONE', #73157 ) ;
#48700=VERTEX_POINT ( 'NONE', #97736 ) ;
#48701=ORIENTED_EDGE ( 'NONE', *, *, #48238, .T. ) ;
#48703=LINE ( 'NONE', #61058, #67146 ) ;
#48704=VECTOR ( 'NONE', #90932, 1000.000000000000227 ) ;
#48705=VECTOR ( 'NONE', #66689, 1000.000000000000227 ) ;
#48706=ORIENTED_EDGE ( 'NONE', *, *, #73020, .T. ) ;
#48708=VECTOR ( 'NONE', #133499, 1000.000000000000000 ) ;
#48709=LINE ( 'NONE', #103764, #87977 ) ;
#48712=EDGE_CURVE ( 'NONE', #51714, #94334, #107867, .T. ) ;
#48713=VERTEX_POINT ( 'NONE', #41205 ) ;
#48714=CARTESIAN_POINT ( 'NONE',  ( -28.49999999999981171, -20.56887692260760048, 4.000000000000000000 ) ) ;
#48715=LINE ( 'NONE', #49460, #123323 ) ;
#48716=ADVANCED_FACE ( 'NONE', ( #128934 ), #141229, .F. ) ;
#48717=CARTESIAN_POINT ( 'NONE',  ( -30.71757738642547508, -21.73023691814492508, 5.000000000000000888 ) ) ;
#48719=CARTESIAN_POINT ( 'NONE',  ( -2.671830600776449405, -21.74070752338406010, 4.000000000000000000 ) ) ;
#48721=CARTESIAN_POINT ( 'NONE',  ( -63.48921356237309510, -27.52281430457099631, 5.000000000000000000 ) ) ;
#48722=DIRECTION ( 'NONE',  ( 0.7071067811865487940, 0.7071067811865463515, 0.000000000000000000 ) ) ;
#48726=DIRECTION ( 'NONE',  ( 0.7071067811865487940, 0.7071067811865463515, -0.000000000000000000 ) ) ;
#48728=ORIENTED_EDGE ( 'NONE', *, *, #112526, .T. ) ;
#48731=ORIENTED_EDGE ( 'NONE', *, *, #38317, .F. ) ;
#48732=EDGE_CURVE ( 'NONE', #108968, #73204, #106426, .T. ) ;
#48733=PLANE ( 'NONE',  #22824 ) ;
#48736=EDGE_LOOP ( 'NONE', ( #130087, #42317, #67761, #72834 ) ) ;
#48738=DIRECTION ( 'NONE',  ( -0.000000000000000000, 0.000000000000000000, 1.000000000000000000 ) ) ;
#48739=EDGE_CURVE ( 'NONE', #96885, #21343, #31772, .T. ) ;
#48740=CARTESIAN_POINT ( 'NONE',  ( 20.99999999999985789, -9.033600742197645417, 5.000000000000000000 ) ) ;
#48741=VECTOR ( 'NONE', #3758, 1000.000000000000000 ) ;
#48742=VECTOR ( 'NONE', #58288, 1000.000000000000000 ) ;
#48744=VERTEX_POINT ( 'NONE', #117322 ) ;
#48746=CARTESIAN_POINT ( 'NONE',  ( -11.99999999999993427, -16.02097659208073566, -11.96015758381206417 ) ) ;
#48748=PLANE ( 'NONE',  #75135 ) ;
#48750=VECTOR ( 'NONE', #40162, 1000.000000000000227 ) ;
#48751=DIRECTION ( 'NONE',  ( 0.3543493200069162685, -0.000000000000000000, -0.9351131265310288487 ) ) ;
#48752=PLANE ( 'NONE',  #78859 ) ;
#48753=ORIENTED_EDGE ( 'NONE', *, *, #65120, .T. ) ;
#48754=ORIENTED_EDGE ( 'NONE', *, *, #77919, .F. ) ;
#48755=LINE ( 'NONE', #126300, #9969 ) ;
#48756=CARTESIAN_POINT ( 'NONE',  ( 34.92499999999998295, 21.72500000000000142, 4.165035510187005130 ) ) ;
#48757=CARTESIAN_POINT ( 'NONE',  ( 26.99999999999980815, 12.25461709320623349, -10.07315571508691043 ) ) ;
#48758=ADVANCED_FACE ( 'NONE', ( #118019 ), #51394, .F. ) ;
#48759=LINE ( 'NONE', #125614, #32454 ) ;
#48760=ADVANCED_FACE ( 'NONE', ( #84722 ), #18723, .F. ) ;
#48763=EDGE_LOOP ( 'NONE', ( #124374, #42838, #139439, #31603 ) ) ;
#48764=DIRECTION ( 'NONE',  ( -0.7071067811865486830, -0.7071067811865464625, -0.000000000000000000 ) ) ;
#48766=LINE ( 'NONE', #92969, #117519 ) ;
#48767=EDGE_LOOP ( 'NONE', ( #47707, #55899, #39126 ) ) ;
#48768=ORIENTED_EDGE ( 'NONE', *, *, #17937, .F. ) ;
#48769=AXIS2_PLACEMENT_3D ( 'NONE', #106432, #50667, #139123 ) ;
#48770=CARTESIAN_POINT ( 'NONE',  ( -31.00193056682077497, -22.22500000000000142, 4.500000000000000888 ) ) ;
#48771=VERTEX_POINT ( 'NONE', #137658 ) ;
#48772=EDGE_CURVE ( 'NONE', #103277, #24958, #4931, .T. ) ;
#48773=EDGE_CURVE ( 'NONE', #27078, #94753, #104267, .T. ) ;
#48774=DIRECTION ( 'NONE',  ( 0.6830127018922181881, 0.6830127018922202975, -0.2588190451025214056 ) ) ;
#48776=LINE ( 'NONE', #92242, #72419 ) ;
#48777=LINE ( 'NONE', #92983, #73424 ) ;
#48778=AXIS2_PLACEMENT_3D ( 'NONE', #97085, #107969, #63810 ) ;
#48780=CARTESIAN_POINT ( 'NONE',  ( 11.81601139373100651, 28.73617430169779041, 5.000000000000000000 ) ) ;
#48781=FACE_BOUND ( 'NONE', #25738, .T. ) ;
#48782=EDGE_CURVE ( 'NONE', #34187, #47131, #136923, .T. ) ;
#48783=CARTESIAN_POINT ( 'NONE',  ( 7.603431928946386087, -14.24070752338413648, 19.24067776001727736 ) ) ;
#48785=CARTESIAN_POINT ( 'NONE',  ( 34.45011844616451668, 10.51628081163738671, 5.000000000000000888 ) ) ;
#48786=DIRECTION ( 'NONE',  ( -0.7071067811865487940, 0.7071067811865463515, 0.000000000000000000 ) ) ;
#48787=ORIENTED_EDGE ( 'NONE', *, *, #14029, .T. ) ;
#48788=VECTOR ( 'NONE', #72820, 1000.000000000000000 ) ;
#48789=VECTOR ( 'NONE', #105855, 1000.000000000000000 ) ;
#48790=CARTESIAN_POINT ( 'NONE',  ( 14.99451991528749595, 28.92564299267948513, 4.000000000000000000 ) ) ;
#48791=VERTEX_POINT ( 'NONE', #37631 ) ;
#48792=EDGE_LOOP ( 'NONE', ( #27543, #18055, #118043, #19666 ) ) ;
#48794=EDGE_LOOP ( 'NONE', ( #83403, #94409, #125553, #11205 ) ) ;
#48795=ADVANCED_FACE ( 'NONE', ( #70974 ), #128206, .F. ) ;
#48796=CARTESIAN_POINT ( 'NONE',  ( 8.816011393731004731, 28.73617430169781173, 5.000000000000000000 ) ) ;
#48798=ORIENTED_EDGE ( 'NONE', *, *, #40194, .T. ) ;
#48799=PLANE ( 'NONE',  #134764 ) ;
#48800=VECTOR ( 'NONE', #133049, 1000.000000000000000 ) ;
#48801=EDGE_CURVE ( 'NONE', #138040, #99796, #106388, .T. ) ;
#48803=VECTOR ( 'NONE', #132216, 999.9999999999998863 ) ;
#48805=FACE_OUTER_BOUND ( 'NONE', #110090, .T. ) ;
#48806=FACE_OUTER_BOUND ( 'NONE', #69800, .T. ) ;
#48807=CARTESIAN_POINT ( 'NONE',  ( -23.99451991528749062, 28.92564299267954908, 4.000000000000000000 ) ) ;
#48810=VECTOR ( 'NONE', #105861, 1000.000000000000000 ) ;
#48812=VECTOR ( 'NONE', #84676, 1000.000000000000000 ) ;
#48814=VECTOR ( 'NONE', #43863, 1000.000000000000000 ) ;
#48815=DIRECTION ( 'NONE',  ( 0.7071067811865487940, 0.7071067811865463515, 0.000000000000000000 ) ) ;
#48816=ORIENTED_EDGE ( 'NONE', *, *, #108630, .F. ) ;
#48817=VECTOR ( 'NONE', #133693, 1000.000000000000000 ) ;
#48818=VERTEX_POINT ( 'NONE', #95548 ) ;
#48820=DIRECTION ( 'NONE',  ( 0.7071067811865487940, -0.7071067811865463515, 0.000000000000000000 ) ) ;
#48822=ORIENTED_EDGE ( 'NONE', *, *, #57480, .F. ) ;
#48823=VECTOR ( 'NONE', #77456, 1000.000000000000000 ) ;
#48824=CARTESIAN_POINT ( 'NONE',  ( 9.836528711265433600, 15.75929247661555976, 9.299976744542940210 ) ) ;
#48825=EDGE_CURVE ( 'NONE', #138000, #78104, #60094, .T. ) ;
#48828=CARTESIAN_POINT ( 'NONE',  ( -3.874853806907633924, -14.24070752338413826, 9.401115078912665624 ) ) ;
#48829=ORIENTED_EDGE ( 'NONE', *, *, #135002, .F. ) ;
#48830=VECTOR ( 'NONE', #111705, 1000.000000000000227 ) ;
#48831=DIRECTION ( 'NONE',  ( -0.000000000000000000, -0.3543493200069152693, 0.9351131265310292928 ) ) ;
#48832=CARTESIAN_POINT ( 'NONE',  ( -22.49999999999984013, -4.533600742197690714, 5.000000000000000000 ) ) ;
#48834=PLANE ( 'NONE',  #21819 ) ;
#48835=FACE_OUTER_BOUND ( 'NONE', #17395, .T. ) ;
#48836=ORIENTED_EDGE ( 'NONE', *, *, #25662, .T. ) ;
#48838=ORIENTED_EDGE ( 'NONE', *, *, #51388, .T. ) ;
#48840=CARTESIAN_POINT ( 'NONE',  ( 38.99451991528749062, 28.92564299267965211, 4.000000000000000000 ) ) ;
#48841=CARTESIAN_POINT ( 'NONE',  ( 4.828169399223503078, 18.75929247661552424, 4.000000000000000000 ) ) ;
#48843=VECTOR ( 'NONE', #10406, 1000.000000000000227 ) ;
#48844=VECTOR ( 'NONE', #95256, 1000.000000000000227 ) ;
#48845=VECTOR ( 'NONE', #100073, 999.9999999999998863 ) ;
#48846=CARTESIAN_POINT ( 'NONE',  ( 0.000000000000000000, 0.000000000000000000, 5.000000000000000000 ) ) ;
#48847=DIRECTION ( 'NONE',  ( 0.7071067811865487940, 0.7071067811865463515, -0.000000000000000000 ) ) ;
#48848=LINE ( 'NONE', #37243, #74545 ) ;
#48849=ORIENTED_EDGE ( 'NONE', *, *, #85299, .F. ) ;
#48850=DIRECTION ( 'NONE',  ( -0.000000000000000000, -0.3543493200069153248, -0.9351131265310291818 ) ) ;
#48852=LINE ( 'NONE', #93052, #49370 ) ;
#48854=CARTESIAN_POINT ( 'NONE',  ( 0.000000000000000000, 0.000000000000000000, 5.000000000000000000 ) ) ;
#48855=DIRECTION ( 'NONE',  ( 0.7071067811865487940, 0.7071067811865463515, 0.000000000000000000 ) ) ;
#48856=ORIENTED_EDGE ( 'NONE', *, *, #21860, .F. ) ;
#48857=AXIS2_PLACEMENT_3D ( 'NONE', #38000, #103913, #82228 ) ;
#48858=ORIENTED_EDGE ( 'NONE', *, *, #115815, .T. ) ;
#48861=CARTESIAN_POINT ( 'NONE',  ( -34.92500000000001137, -3.183345613589545486, 4.500000000000000888 ) ) ;
#48863=CARTESIAN_POINT ( 'NONE',  ( -0.1839886062690032631, 28.73617430169787568, 5.000000000000000000 ) ) ;
#48864=DIRECTION ( 'NONE',  ( 0.6830127018922181881, 0.6830127018922202975, -0.2588190451025214056 ) ) ;
#48865=DIRECTION ( 'NONE',  ( -0.7071067811865486830, -0.7071067811865464625, -0.000000000000000000 ) ) ;
#48866=EDGE_LOOP ( 'NONE', ( #114617, #118246, #9651, #29712 ) ) ;
#48867=CARTESIAN_POINT ( 'NONE',  ( 21.18398860626899349, 28.73617430169802134, 5.000000000000000000 ) ) ;
#48868=VECTOR ( 'NONE', #127339, 1000.000000000000000 ) ;
#48869=LINE ( 'NONE', #3193, #12167 ) ;
#48870=AXIS2_PLACEMENT_3D ( 'NONE', #31905, #63135, #130523 ) ;
#48873=PLANE ( 'NONE',  #25543 ) ;
#48874=VERTEX_POINT ( 'NONE', #92687 ) ;
#48875=LINE ( 'NONE', #80788, #136689 ) ;
#48876=ORIENTED_EDGE ( 'NONE', *, *, #25974, .F. ) ;
#48877=EDGE_CURVE ( 'NONE', #106116, #74581, #105690, .T. ) ;
#48878=ORIENTED_EDGE ( 'NONE', *, *, #40578, .F. ) ;
#48879=VECTOR ( 'NONE', #134612, 1000.000000000000227 ) ;
#48880=LINE ( 'NONE', #83669, #47885 ) ;
#48881=CARTESIAN_POINT ( 'NONE',  ( -18.18398860626898994, 28.73617430169800002, 5.000000000000000000 ) ) ;
#48883=EDGE_CURVE ( 'NONE', #24156, #48700, #115129, .T. ) ;
#48884=DIRECTION ( 'NONE',  ( 0.7071067811865487940, -0.7071067811865463515, 0.000000000000000000 ) ) ;
#48885=DIRECTION ( 'NONE',  ( -0.000000000000000000, 0.000000000000000000, 1.000000000000000000 ) ) ;
#48887=EDGE_CURVE ( 'NONE', #133571, #30937, #115846, .T. ) ;
#48888=EDGE_LOOP ( 'NONE', ( #127696, #42435, #105177, #86595 ) ) ;
#48890=CARTESIAN_POINT ( 'NONE',  ( -13.82816939922342492, 18.75929247661553489, 4.000000000000000000 ) ) ;
#48893=DIRECTION ( 'NONE',  ( -0.000000000000000000, 0.000000000000000000, 1.000000000000000000 ) ) ;
#48894=FACE_OUTER_BOUND ( 'NONE', #3449, .T. ) ;
#48896=EDGE_CURVE ( 'NONE', #22343, #40695, #127470, .T. ) ;
#48898=EDGE_CURVE ( 'NONE', #37768, #109138, #39782, .T. ) ;
#48899=LINE ( 'NONE', #93103, #36921 ) ;
#48900=ORIENTED_EDGE ( 'NONE', *, *, #76566, .F. ) ;
#48901=ORIENTED_EDGE ( 'NONE', *, *, #121425, .F. ) ;
#48903=PLANE ( 'NONE',  #132711 ) ;
#48905=PLANE ( 'NONE',  #115650 ) ;
#48906=DIRECTION ( 'NONE',  ( 1.000000000000000000, 0.000000000000000000, 0.000000000000000000 ) ) ;
#48907=ORIENTED_EDGE ( 'NONE', *, *, #74431, .F. ) ;
#48910=VECTOR ( 'NONE', #41656, 999.9999999999998863 ) ;
#48911=EDGE_CURVE ( 'NONE', #47009, #29818, #116597, .T. ) ;
#48913=CARTESIAN_POINT ( 'NONE',  ( 6.938893903907228378E-15, 5.587461875839191627, 4.000000000000000000 ) ) ;
#48915=FACE_OUTER_BOUND ( 'NONE', #29157, .T. ) ;
#48916=ORIENTED_EDGE ( 'NONE', *, *, #30250, .F. ) ;
#48918=ORIENTED_EDGE ( 'NONE', *, *, #104030, .F. ) ;
#48919=AXIS2_PLACEMENT_3D ( 'NONE', #85058, #110356, #11032 ) ;
#48920=VECTOR ( 'NONE', #83454, 1000.000000000000000 ) ;
#48921=AXIS2_PLACEMENT_3D ( 'NONE', #71757, #41233, #17344 ) ;
#48922=CARTESIAN_POINT ( 'NONE',  ( 11.51078643762690490, -27.52281430457047406, 5.000000000000000000 ) ) ;
#48923=DIRECTION ( 'NONE',  ( 0.7071067811865486830, -0.7071067811865464625, -0.000000000000000000 ) ) ;
#48925=LINE ( 'NONE', #93128, #34984 ) ;
#48926=DIRECTION ( 'NONE',  ( 0.7071067811865486830, -0.7071067811865464625, -0.000000000000000000 ) ) ;
#48927=ORIENTED_EDGE ( 'NONE', *, *, #120926, .T. ) ;
#48929=CARTESIAN_POINT ( 'NONE',  ( -20.81601139373100295, 28.73617430169773002, 5.000000000000000000 ) ) ;
#48930=LINE ( 'NONE', #82977, #33287 ) ;
#48931=AXIS2_PLACEMENT_3D ( 'NONE', #74969, #75662, #108966 ) ;
#48932=EDGE_CURVE ( 'NONE', #75514, #110346, #76694, .T. ) ;
#48933=ORIENTED_EDGE ( 'NONE', *, *, #132574, .T. ) ;
#48934=ORIENTED_EDGE ( 'NONE', *, *, #101446, .F. ) ;
#48935=VECTOR ( 'NONE', #71428, 1000.000000000000114 ) ;
#48936=FACE_OUTER_BOUND ( 'NONE', #49292, .T. ) ;
#48937=CARTESIAN_POINT ( 'NONE',  ( 14.99451991528749595, 28.92564299267948513, 4.000000000000000000 ) ) ;
#48938=EDGE_CURVE ( 'NONE', #84739, #105871, #75951, .T. ) ;
#48942=ORIENTED_EDGE ( 'NONE', *, *, #80247, .F. ) ;
#48943=CARTESIAN_POINT ( 'NONE',  ( 17.81601139373099940, 28.73617430169775133, 5.000000000000000000 ) ) ;
#48945=AXIS2_PLACEMENT_3D ( 'NONE', #75696, #79306, #45237 ) ;
#48946=EDGE_CURVE ( 'NONE', #106292, #43835, #32453, .T. ) ;
#48947=ORIENTED_EDGE ( 'NONE', *, *, #23256, .T. ) ;
#48948=VECTOR ( 'NONE', #23033, 1000.000000000000000 ) ;
#48950=EDGE_CURVE ( 'NONE', #49613, #9752, #107137, .T. ) ;
#48952=LINE ( 'NONE', #82297, #52537 ) ;
#48953=FACE_OUTER_BOUND ( 'NONE', #116648, .T. ) ;
#48954=AXIS2_PLACEMENT_3D ( 'NONE', #36064, #136064, #1933 ) ;
#48955=EDGE_CURVE ( 'NONE', #108205, #14902, #131049, .T. ) ;
#48956=FACE_BOUND ( 'NONE', #135735, .T. ) ;
#48957=VECTOR ( 'NONE', #69755, 1000.000000000000227 ) ;
#48958=DIRECTION ( 'NONE',  ( -0.000000000000000000, 0.000000000000000000, 1.000000000000000000 ) ) ;
#48959=CARTESIAN_POINT ( 'NONE',  ( -34.92500000000001137, -3.425372908132398475, 14.71988515618267357 ) ) ;
#48960=CARTESIAN_POINT ( 'NONE',  ( -18.48921356237309510, -27.52281430457068367, 5.000000000000000000 ) ) ;
#48961=PLANE ( 'NONE',  #73656 ) ;
#48962=EDGE_CURVE ( 'NONE', #112402, #105677, #9967, .T. ) ;
#48963=CARTESIAN_POINT ( 'NONE',  ( -60.18398860626900415, 28.73617430169829490, 5.000000000000000000 ) ) ;
#48965=ORIENTED_EDGE ( 'NONE', *, *, #38682, .T. ) ;
#48966=ORIENTED_EDGE ( 'NONE', *, *, #89146, .T. ) ;
#48972=CARTESIAN_POINT ( 'NONE',  ( 30.48921356237309510, -27.52281430457076894, 5.000000000000000000 ) ) ;
#48973=DIRECTION ( 'NONE',  ( -0.7071067811865487940, 0.7071067811865463515, 0.000000000000000000 ) ) ;
#48974=DIRECTION ( 'NONE',  ( -0.000000000000000000, -0.3543493200069153248, -0.9351131265310291818 ) ) ;
#48975=EDGE_LOOP ( 'NONE', ( #98345, #12061, #69951, #55153 ) ) ;
#48976=CARTESIAN_POINT ( 'NONE',  ( 33.83652871126528794, 15.75929247661555443, 9.299976744542998830 ) ) ;
#48978=DIRECTION ( 'NONE',  ( 0.7071067811865487940, 0.7071067811865463515, -0.000000000000000000 ) ) ;
#48979=CARTESIAN_POINT ( 'NONE',  ( -8.292893218813398803, 2.259292476615692546, 5.000000000000000000 ) ) ;
#48980=CARTESIAN_POINT ( 'NONE',  ( 18.29974487139159223, -27.71228299555219010, 4.000000000000000000 ) ) ;
#48981=CARTESIAN_POINT ( 'NONE',  ( -11.99999999999992006, 5.587461875839191627, 4.000000000000000000 ) ) ;
#48982=VECTOR ( 'NONE', #51884, 1000.000000000000000 ) ;
#48983=CARTESIAN_POINT ( 'NONE',  ( -26.99999999999981171, -22.06887692260758982, 4.000000000000000000 ) ) ;
#48985=DIRECTION ( 'NONE',  ( 0.6830127018922181881, 0.6830127018922202975, -0.2588190451025214056 ) ) ;
#48986=CARTESIAN_POINT ( 'NONE',  ( -5.816011393731002066, 28.73617430169783304, 5.000000000000000000 ) ) ;
#48987=ORIENTED_EDGE ( 'NONE', *, *, #56983, .T. ) ;
#48988=ADVANCED_FACE ( 'NONE', ( #140480 ), #141188, .F. ) ;
#48989=ORIENTED_EDGE ( 'NONE', *, *, #15685, .F. ) ;
#48990=ORIENTED_EDGE ( 'NONE', *, *, #21382, .F. ) ;
#48992=ORIENTED_EDGE ( 'NONE', *, *, #104573, .F. ) ;
#48993=ADVANCED_FACE ( 'NONE', ( #98420 ), #131768, .F. ) ;
#48996=ORIENTED_EDGE ( 'NONE', *, *, #106370, .T. ) ;
#48997=LINE ( 'NONE', #102669, #27112 ) ;
#48998=ORIENTED_EDGE ( 'NONE', *, *, #108330, .T. ) ;
#48999=PLANE ( 'NONE',  #39617 ) ;
#49001=VECTOR ( 'NONE', #106217, 999.9999999999998863 ) ;
#49002=VECTOR ( 'NONE', #50612, 999.9999999999998863 ) ;
#49003=CARTESIAN_POINT ( 'NONE',  ( -12.08491323193754141, -12.74070752338414891, 18.74364270924351317 ) ) ;
#49004=VERTEX_POINT ( 'NONE', #107834 ) ;
#49006=EDGE_CURVE ( 'NONE', #81784, #93258, #132515, .T. ) ;
#49007=FACE_OUTER_BOUND ( 'NONE', #57773, .T. ) ;
#49008=FACE_OUTER_BOUND ( 'NONE', #62960, .T. ) ;
#49009=AXIS2_PLACEMENT_3D ( 'NONE', #40789, #84991, #129193 ) ;
#49010=AXIS2_PLACEMENT_3D ( 'NONE', #142391, #75005, #130079 ) ;
#49013=DIRECTION ( 'NONE',  ( -0.000000000000000000, 0.3543493200069153248, 0.9351131265310292928 ) ) ;
#49014=ORIENTED_EDGE ( 'NONE', *, *, #124383, .T. ) ;
#49015=VERTEX_POINT ( 'NONE', #54926 ) ;
#49016=ORIENTED_EDGE ( 'NONE', *, *, #114527, .F. ) ;
#49017=EDGE_LOOP ( 'NONE', ( #29624, #27190, #137940, #46637, #131158 ) ) ;
#49018=CARTESIAN_POINT ( 'NONE',  ( -17.99999999999986855, -6.108550654416975867, -3.114665004255009695 ) ) ;
#49019=VECTOR ( 'NONE', #99092, 999.9999999999998863 ) ;
#49022=VECTOR ( 'NONE', #56463, 1000.000000000000000 ) ;
#49023=VECTOR ( 'NONE', #84609, 1000.000000000000000 ) ;
#49024=LINE ( 'NONE', #71477, #51530 ) ;
#49025=DIRECTION ( 'NONE',  ( -0.000000000000000000, 0.000000000000000000, 1.000000000000000000 ) ) ;
#49026=CARTESIAN_POINT ( 'NONE',  ( 29.99999999999979039, 13.55218569542902429, 5.000000000000000000 ) ) ;
#49027=ADVANCED_FACE ( 'NONE', ( #65834 ), #75262, .F. ) ;
#49028=DIRECTION ( 'NONE',  ( -0.7071067811865486830, -0.7071067811865464625, 0.000000000000000000 ) ) ;
#49029=EDGE_LOOP ( 'NONE', ( #17349, #114942, #68398, #65377 ) ) ;
#49030=DIRECTION ( 'NONE',  ( 0.7071067811865487940, 0.7071067811865463515, -0.000000000000000000 ) ) ;
#49032=FACE_OUTER_BOUND ( 'NONE', #131658, .T. ) ;
#49036=ORIENTED_EDGE ( 'NONE', *, *, #105482, .F. ) ;
#49037=ORIENTED_EDGE ( 'NONE', *, *, #40780, .F. ) ;
#49038=DIRECTION ( 'NONE',  ( 1.000000000000000000, 0.000000000000000000, 0.000000000000000000 ) ) ;
#49041=DIRECTION ( 'NONE',  ( -0.7071067811865487940, 0.7071067811865463515, -0.000000000000000000 ) ) ;
#49042=CARTESIAN_POINT ( 'NONE',  ( -34.92500000000001137, 21.72500000000000142, 5.000000000000000000 ) ) ;
#49043=CARTESIAN_POINT ( 'NONE',  ( -27.79289321881326558, 12.75929247661558996, 5.000000000000000000 ) ) ;
#49045=VECTOR ( 'NONE', #110958, 1000.000000000000000 ) ;
#49046=LINE ( 'NONE', #103381, #51016 ) ;
#49047=VECTOR ( 'NONE', #66419, 1000.000000000000227 ) ;
#49049=DIRECTION ( 'NONE',  ( 0.7071067811865487940, 0.7071067811865463515, 0.000000000000000000 ) ) ;
#49050=CARTESIAN_POINT ( 'NONE',  ( -48.18398860626899705, 28.73617430169820608, 5.000000000000000000 ) ) ;
#49052=CARTESIAN_POINT ( 'NONE',  ( 5.241399257802002332, 21.72500000000000853, 5.000000000000000000 ) ) ;
#49054=LINE ( 'NONE', #84541, #89304 ) ;
#49055=AXIS2_PLACEMENT_3D ( 'NONE', #128429, #61757, #42858 ) ;
#49057=DIRECTION ( 'NONE',  ( -0.7071067811865486830, -0.7071067811865464625, -0.000000000000000000 ) ) ;
#49058=CARTESIAN_POINT ( 'NONE',  ( -19.77325839282154263, -11.24070752338416845, 18.24660765846978094 ) ) ;
#49059=EDGE_LOOP ( 'NONE', ( #6241, #36303, #24628, #2088 ) ) ;
#49060=DIRECTION ( 'NONE',  ( 1.000000000000000000, 0.000000000000000000, 0.000000000000000000 ) ) ;
#49061=DIRECTION ( 'NONE',  ( 0.3543493200069162685, -0.000000000000000000, -0.9351131265310288487 ) ) ;
#49062=EDGE_CURVE ( 'NONE', #71184, #140269, #30302, .T. ) ;
#49063=ADVANCED_FACE ( 'NONE', ( #33200 ), #52750, .T. ) ;
#49064=VERTEX_POINT ( 'NONE', #65098 ) ;
#49065=DIRECTION ( 'NONE',  ( -0.7071067811865486830, 0.7071067811865464625, 0.000000000000000000 ) ) ;
#49067=DIRECTION ( 'NONE',  ( 0.7071067811865486830, -0.7071067811865464625, -0.000000000000000000 ) ) ;
#49069=ORIENTED_EDGE ( 'NONE', *, *, #14565, .T. ) ;
#49071=CARTESIAN_POINT ( 'NONE',  ( 5.282422613574296655, -21.73023691814493930, 5.000000000000000888 ) ) ;
#49072=ADVANCED_FACE ( 'NONE', ( #52062 ), #64362, .F. ) ;
#49074=EDGE_CURVE ( 'NONE', #79378, #99520, #31036, .T. ) ;
#49075=DIRECTION ( 'NONE',  ( 0.7071067811865487940, 0.7071067811865463515, 0.000000000000000000 ) ) ;
#49077=ORIENTED_EDGE ( 'NONE', *, *, #124828, .F. ) ;
#49078=EDGE_CURVE ( 'NONE', #35299, #92701, #53490, .T. ) ;
#49079=DIRECTION ( 'NONE',  ( -0.6830127018922181881, 0.6830127018922202975, -0.2588190451025214056 ) ) ;
#49080=EDGE_CURVE ( 'NONE', #49508, #68079, #1902, .T. ) ;
#49081=FACE_OUTER_BOUND ( 'NONE', #145, .T. ) ;
#49085=DIRECTION ( 'NONE',  ( -0.000000000000000000, 0.3543493200069153248, 0.9351131265310292928 ) ) ;
#49088=LINE ( 'NONE', #124481, #44484 ) ;
#49089=EDGE_CURVE ( 'NONE', #73688, #20599, #79575, .T. ) ;
#49090=VERTEX_POINT ( 'NONE', #46946 ) ;
#49092=CARTESIAN_POINT ( 'NONE',  ( -21.18398860626899349, 28.73617430169802134, 5.000000000000000000 ) ) ;
#49093=LINE ( 'NONE', #49815, #90935 ) ;
#49095=DIRECTION ( 'NONE',  ( -0.7071067811865486830, 0.7071067811865464625, 0.000000000000000000 ) ) ;
#49096=ORIENTED_EDGE ( 'NONE', *, *, #81629, .T. ) ;
#49097=DIRECTION ( 'NONE',  ( -0.7071067811865487940, 0.7071067811865463515, -0.000000000000000000 ) ) ;
#49098=ADVANCED_FACE ( 'NONE', ( #57797 ), #23708, .F. ) ;
#49099=PLANE ( 'NONE',  #125284 ) ;
#49101=CARTESIAN_POINT ( 'NONE',  ( -54.18398860626899705, 28.73617430169825226, 5.000000000000000000 ) ) ;
#49102=DIRECTION ( 'NONE',  ( 0.7071067811865487940, -0.7071067811865463515, 0.000000000000000000 ) ) ;
#49103=ORIENTED_EDGE ( 'NONE', *, *, #6187, .T. ) ;
#49104=CARTESIAN_POINT ( 'NONE',  ( -15.29974487139158867, -27.71228299555216879, 4.000000000000000000 ) ) ;
#49105=CARTESIAN_POINT ( 'NONE',  ( 20.99999999999985079, 9.631307414974342507, -9.079085613539490396 ) ) ;
#49108=EDGE_CURVE ( 'NONE', #87414, #103176, #36039, .T. ) ;
#49110=ORIENTED_EDGE ( 'NONE', *, *, #125128, .T. ) ;
#49111=VERTEX_POINT ( 'NONE', #88987 ) ;
#49112=ORIENTED_EDGE ( 'NONE', *, *, #99993, .F. ) ;
#49114=EDGE_LOOP ( 'NONE', ( #98127, #106171, #72461, #2914 ) ) ;
#49118=CARTESIAN_POINT ( 'NONE',  ( -12.79289321881337216, 12.75929247661558463, 5.000000000000000000 ) ) ;
#49119=VERTEX_POINT ( 'NONE', #11360 ) ;
#49121=VECTOR ( 'NONE', #56644, 1000.000000000000000 ) ;
#49122=FACE_OUTER_BOUND ( 'NONE', #13416, .T. ) ;
#49123=CARTESIAN_POINT ( 'NONE',  ( 30.48921356237309510, -27.52281430457076894, 5.000000000000000000 ) ) ;
#49124=VECTOR ( 'NONE', #4154, 1000.000000000000000 ) ;
#49125=VECTOR ( 'NONE', #94400, 1000.000000000000227 ) ;
#49127=CARTESIAN_POINT ( 'NONE',  ( 24.51665438641027350, 22.22500000000000142, 4.500000000000000888 ) ) ;
#49129=VECTOR ( 'NONE', #85975, 1000.000000000000000 ) ;
#49130=CARTESIAN_POINT ( 'NONE',  ( 11.99451991528749417, 28.92564299267946382, 4.000000000000000000 ) ) ;
#49132=VECTOR ( 'NONE', #4768, 1000.000000000000000 ) ;
#49133=EDGE_CURVE ( 'NONE', #18399, #12755, #91809, .T. ) ;
#49134=ORIENTED_EDGE ( 'NONE', *, *, #107557, .F. ) ;
#49135=VERTEX_POINT ( 'NONE', #136034 ) ;
#49136=DIRECTION ( 'NONE',  ( -0.3543493200069163240, -0.000000000000000000, -0.9351131265310288487 ) ) ;
#49137=CARTESIAN_POINT ( 'NONE',  ( 34.92499999999998295, 12.75929247661558996, 4.255531930566172072 ) ) ;
#49138=DIRECTION ( 'NONE',  ( 0.6830127018922180770, -0.6830127018922204085, -0.2588190451025213501 ) ) ;
#49139=DIRECTION ( 'NONE',  ( -0.7071067811865487940, 0.7071067811865463515, 0.000000000000000000 ) ) ;
#49140=DIRECTION ( 'NONE',  ( -0.3543493200069162685, -0.000000000000000000, -0.9351131265310288487 ) ) ;
#49141=ADVANCED_FACE ( 'NONE', ( #113556 ), #13516, .T. ) ;
#49142=LINE ( 'NONE', #117722, #111412 ) ;
#49143=CARTESIAN_POINT ( 'NONE',  ( 16.35824297541129368, 15.75929247661555088, 19.34181609438695659 ) ) ;
#49144=ORIENTED_EDGE ( 'NONE', *, *, #96802, .F. ) ;
#49145=VERTEX_POINT ( 'NONE', #124447 ) ;
#49147=EDGE_CURVE ( 'NONE', #74780, #6489, #22954, .T. ) ;
#49148=VERTEX_POINT ( 'NONE', #111420 ) ;
#49149=VECTOR ( 'NONE', #444, 1000.000000000000227 ) ;
#49151=ORIENTED_EDGE ( 'NONE', *, *, #85407, .F. ) ;
#49153=EDGE_CURVE ( 'NONE', #96833, #94758, #69376, .T. ) ;
#49154=VECTOR ( 'NONE', #54375, 1000.000000000000000 ) ;
#49155=DIRECTION ( 'NONE',  ( -0.7071067811865486830, -0.7071067811865464625, -0.000000000000000000 ) ) ;
#49156=DIRECTION ( 'NONE',  ( -0.7071067811865486830, -0.7071067811865464625, -0.000000000000000000 ) ) ;
#49157=VECTOR ( 'NONE', #141998, 999.9999999999998863 ) ;
#49159=VERTEX_POINT ( 'NONE', #112164 ) ;
#49160=DIRECTION ( 'NONE',  ( -0.3543493200069162685, -0.000000000000000000, -0.9351131265310288487 ) ) ;
#49161=CARTESIAN_POINT ( 'NONE',  ( 8.999999999999934275, -15.03360074219758502, 5.000000000000000000 ) ) ;
#49162=ORIENTED_EDGE ( 'NONE', *, *, #130775, .T. ) ;
#49163=LINE ( 'NONE', #138297, #4049 ) ;
#49165=ORIENTED_EDGE ( 'NONE', *, *, #34285, .F. ) ;
#49167=DIRECTION ( 'NONE',  ( 2.781805975412905274E-17, -0.3543493200069152138, 0.9351131265310292928 ) ) ;
#49168=EDGE_LOOP ( 'NONE', ( #79003, #13858, #86503, #138143 ) ) ;
#49169=EDGE_LOOP ( 'NONE', ( #15091, #135910, #108848 ) ) ;
#49171=AXIS2_PLACEMENT_3D ( 'NONE', #8787, #86427, #30621 ) ;
#49172=VERTEX_POINT ( 'NONE', #121579 ) ;
#49173=LINE ( 'NONE', #60044, #21088 ) ;
#49174=ADVANCED_FACE ( 'NONE', ( #89675 ), #34593, .T. ) ;
#49175=LINE ( 'NONE', #73756, #24210 ) ;
#49177=LINE ( 'NONE', #38285, #105063 ) ;
#49178=LINE ( 'NONE', #4148, #115363 ) ;
#49179=VECTOR ( 'NONE', #85116, 1000.000000000000227 ) ;
#49180=CARTESIAN_POINT ( 'NONE',  ( 40.60343192894618625, -14.24070752338413293, 19.24067776001735197 ) ) ;
#49181=DIRECTION ( 'NONE',  ( -0.7071067811865486830, -0.7071067811865464625, -0.000000000000000000 ) ) ;
#49182=CARTESIAN_POINT ( 'NONE',  ( -14.20710678118644665, 18.75929247661552779, 5.000000000000000000 ) ) ;
#49185=FACE_OUTER_BOUND ( 'NONE', #35544, .T. ) ;
#49186=LINE ( 'NONE', #57934, #131644 ) ;
#49187=ORIENTED_EDGE ( 'NONE', *, *, #71866, .T. ) ;
#49188=ADVANCED_FACE ( 'NONE', ( #12814 ), #101264, .T. ) ;
#49190=CARTESIAN_POINT ( 'NONE',  ( 24.29974487139158867, -27.71228299555223273, 4.000000000000000000 ) ) ;
#49191=ORIENTED_EDGE ( 'NONE', *, *, #111940, .F. ) ;
#49194=DIRECTION ( 'NONE',  ( 4.681814790819592407E-17, 0.3543493200069153248, 0.9351131265310292928 ) ) ;
#49195=AXIS2_PLACEMENT_3D ( 'NONE', #70365, #103628, #8568 ) ;
#49196=ORIENTED_EDGE ( 'NONE', *, *, #12077, .F. ) ;
#49197=( BOUNDED_CURVE ( )  B_SPLINE_CURVE ( 3, ( #83771, #104024, #71443, #117059 ),
 .UNSPECIFIED., .F., .T. ) 
 B_SPLINE_CURVE_WITH_KNOTS ( ( 4, 4 ),
 ( 2.779374508378135378, 4.199602562396838934 ),
 .UNSPECIFIED. ) 
 CURVE ( )  GEOMETRIC_REPRESENTATION_ITEM ( )  RATIONAL_B_SPLINE_CURVE ( ( 1.000000000000000000, 0.8388583629366628269, 0.8388583629366628269, 1.000000000000000000 ) ) 
 REPRESENTATION_ITEM ( '' )  );
#49198=DIRECTION ( 'NONE',  ( -0.6830127018922180770, -0.6830127018922204085, -0.2588190451025213501 ) ) ;
#49200=PLANE ( 'NONE',  #23203 ) ;
#49201=ADVANCED_FACE ( 'NONE', ( #35332 ), #114956, .F. ) ;
#49202=CARTESIAN_POINT ( 'NONE',  ( -15.13014816246815286, 7.677378749015543846, 4.326165144404733098 ) ) ;
#49203=ORIENTED_EDGE ( 'NONE', *, *, #9676, .F. ) ;
#49205=VECTOR ( 'NONE', #24110, 1000.000000000000000 ) ;
#49206=VERTEX_POINT ( 'NONE', #138914 ) ;
#49207=PLANE ( 'NONE',  #65372 ) ;
#49209=CARTESIAN_POINT ( 'NONE',  ( -19.49999999999985789, 19.46639925780205971, 5.000000000000000000 ) ) ;
#49210=CARTESIAN_POINT ( 'NONE',  ( -5.999999999999952927, 8.587461875839151659, 4.000000000000000000 ) ) ;
#49211=CARTESIAN_POINT ( 'NONE',  ( 5.999999999999956479, 16.93112307739201583, 4.000000000000000000 ) ) ;
#49212=EDGE_LOOP ( 'NONE', ( #17482, #50138, #124789, #141130, #56466 ) ) ;
#49213=VERTEX_POINT ( 'NONE', #116435 ) ;
#49214=ORIENTED_EDGE ( 'NONE', *, *, #1487, .F. ) ;
#49215=CARTESIAN_POINT ( 'NONE',  ( -34.91107144025656339, 21.84219451764876396, 4.000000000000000000 ) ) ;
#49216=LINE ( 'NONE', #16537, #127437 ) ;
#49217=VECTOR ( 'NONE', #59407, 1000.000000000000000 ) ;
#49218=VECTOR ( 'NONE', #75767, 1000.000000000000000 ) ;
#49219=DIRECTION ( 'NONE',  ( 0.7071067811865486830, -0.7071067811865464625, -0.000000000000000000 ) ) ;
#49221=PLANE ( 'NONE',  #75134 ) ;
#49222=CARTESIAN_POINT ( 'NONE',  ( 34.92499999999998295, 13.70115479773738265, 1.769996414796620954 ) ) ;
#49223=VECTOR ( 'NONE', #140287, 1000.000000000000000 ) ;
#49224=CARTESIAN_POINT ( 'NONE',  ( 28.49999999999980105, 3.653845994658417418, -4.504631822206436098 ) ) ;
#49226=DIRECTION ( 'NONE',  ( 0.3543493200069162685, -0.000000000000000000, -0.9351131265310288487 ) ) ;
#49227=DIRECTION ( 'NONE',  ( 0.7071067811865487940, 0.7071067811865463515, 0.000000000000000000 ) ) ;
#49228=LINE ( 'NONE', #3518, #2795 ) ;
#49229=ORIENTED_EDGE ( 'NONE', *, *, #60258, .T. ) ;
#49230=DIRECTION ( 'NONE',  ( 0.7071067811865487940, 0.7071067811865463515, 0.000000000000000000 ) ) ;
#49231=VECTOR ( 'NONE', #98644, 1000.000000000000227 ) ;
#49232=VECTOR ( 'NONE', #124124, 1000.000000000000000 ) ;
#49234=DIRECTION ( 'NONE',  ( -0.000000000000000000, -0.3543493200069152693, 0.9351131265310292928 ) ) ;
#49235=ORIENTED_EDGE ( 'NONE', *, *, #100398, .F. ) ;
#49236=CARTESIAN_POINT ( 'NONE',  ( 47.99451991528749062, 28.92564299267971251, 4.000000000000000000 ) ) ;
#49237=LINE ( 'NONE', #36891, #83368 ) ;
#49238=ORIENTED_EDGE ( 'NONE', *, *, #135902, .T. ) ;
#49239=ORIENTED_EDGE ( 'NONE', *, *, #92070, .T. ) ;
#49240=CARTESIAN_POINT ( 'NONE',  ( -39.18398860626899705, 28.73617430169814568, 5.000000000000000000 ) ) ;
#49241=CARTESIAN_POINT ( 'NONE',  ( -5.994519915287488843, 28.92564299267942118, 4.000000000000000000 ) ) ;
#49242=DIRECTION ( 'NONE',  ( -0.7071067811865486830, 0.7071067811865464625, 0.000000000000000000 ) ) ;
#49243=ORIENTED_EDGE ( 'NONE', *, *, #32077, .F. ) ;
#49244=PLANE ( 'NONE',  #32777 ) ;
#49245=VERTEX_POINT ( 'NONE', #71509 ) ;
#49246=PLANE ( 'NONE',  #24385 ) ;
#49247=CARTESIAN_POINT ( 'NONE',  ( -4.499999999999967137, -13.53360074219760101, 5.000000000000000000 ) ) ;
#49249=EDGE_CURVE ( 'NONE', #101316, #49712, #125161, .T. ) ;
#49250=CARTESIAN_POINT ( 'NONE',  ( -12.18398860626900060, 28.73617430169795739, 5.000000000000000000 ) ) ;
#49251=VECTOR ( 'NONE', #90748, 1000.000000000000000 ) ;
#49252=CARTESIAN_POINT ( 'NONE',  ( 24.08314806772916228, 21.75929247661548871, 7.311836541448109017 ) ) ;
#49253=EDGE_CURVE ( 'NONE', #17479, #58130, #139649, .T. ) ;
#49254=LINE ( 'NONE', #80447, #104726 ) ;
#49255=CARTESIAN_POINT ( 'NONE',  ( 66.18398860626901126, 28.73617430169833753, 5.000000000000000000 ) ) ;
#49256=EDGE_CURVE ( 'NONE', #70917, #67449, #138189, .T. ) ;
#49257=DIRECTION ( 'NONE',  ( 0.7071067811865487940, 0.7071067811865463515, 0.000000000000000000 ) ) ;
#49260=LINE ( 'NONE', #138379, #101505 ) ;
#49261=CARTESIAN_POINT ( 'NONE',  ( 16.49999999999989697, -4.912538124160701791, 4.000000000000000000 ) ) ;
#49262=CARTESIAN_POINT ( 'NONE',  ( 0.000000000000000000, 0.000000000000000000, 5.000000000000000000 ) ) ;
#49263=ADVANCED_FACE ( 'NONE', ( #106233 ), #83094, .F. ) ;
#49264=ORIENTED_EDGE ( 'NONE', *, *, #21015, .F. ) ;
#49266=EDGE_LOOP ( 'NONE', ( #101704, #117316, #102713, #54859 ) ) ;
#49268=ORIENTED_EDGE ( 'NONE', *, *, #83139, .T. ) ;
#49269=ORIENTED_EDGE ( 'NONE', *, *, #99636, .T. ) ;
#49271=EDGE_CURVE ( 'NONE', #87588, #119333, #92513, .T. ) ;
#49274=AXIS2_PLACEMENT_3D ( 'NONE', #42332, #131467, #119832 ) ;
#49276=DIRECTION ( 'NONE',  ( -0.7071067811865486830, 0.7071067811865464625, 0.000000000000000000 ) ) ;
#49277=VERTEX_POINT ( 'NONE', #94655 ) ;
#49278=FACE_OUTER_BOUND ( 'NONE', #82555, .T. ) ;
#49279=CARTESIAN_POINT ( 'NONE',  ( -45.18398860626900415, 28.73617430169818832, 5.000000000000000000 ) ) ;
#49280=EDGE_CURVE ( 'NONE', #118878, #81113, #59237, .T. ) ;
#49281=CARTESIAN_POINT ( 'NONE',  ( 31.96659967656958301, 6.759292476615653023, 12.28218704918529447 ) ) ;
#49283=EDGE_CURVE ( 'NONE', #130144, #67630, #70811, .T. ) ;
#49284=DIRECTION ( 'NONE',  ( 1.000000000000000000, 0.000000000000000000, 0.000000000000000000 ) ) ;
#49285=CARTESIAN_POINT ( 'NONE',  ( 0.000000000000000000, 0.000000000000000000, 5.000000000000000000 ) ) ;
#49286=CARTESIAN_POINT ( 'NONE',  ( 5.207106781186512379, -2.240707523384262601, 5.000000000000000000 ) ) ;
#49287=FACE_OUTER_BOUND ( 'NONE', #47500, .T. ) ;
#49288=DIRECTION ( 'NONE',  ( -0.6830127018922180770, -0.6830127018922204085, -0.2588190451025213501 ) ) ;
#49289=CARTESIAN_POINT ( 'NONE',  ( 25.17183060077629975, 12.75929247661558641, 4.000000000000000000 ) ) ;
#49290=ADVANCED_FACE ( 'NONE', ( #83841 ), #39609, .T. ) ;
#49291=DIRECTION ( 'NONE',  ( -0.7071067811865486830, 0.7071067811865464625, 0.000000000000000000 ) ) ;
#49292=EDGE_LOOP ( 'NONE', ( #27525, #27035, #135303, #72249 ) ) ;
#49293=VERTEX_POINT ( 'NONE', #26568 ) ;
#49295=VERTEX_POINT ( 'NONE', #17803 ) ;
#49297=EDGE_CURVE ( 'NONE', #133341, #139662, #82391, .T. ) ;
#49298=AXIS2_PLACEMENT_3D ( 'NONE', #133074, #33061, #9827 ) ;
#49299=CARTESIAN_POINT ( 'NONE',  ( 32.67183060077624646, 5.259292476615669010, 4.000000000000000000 ) ) ;
#49300=ORIENTED_EDGE ( 'NONE', *, *, #122910, .F. ) ;
#49301=DIRECTION ( 'NONE',  ( 0.7071067811865487940, 0.7071067811865463515, 0.000000000000000000 ) ) ;
#49302=DIRECTION ( 'NONE',  ( -0.3543493200069162685, -0.000000000000000000, -0.9351131265310288487 ) ) ;
#49304=VERTEX_POINT ( 'NONE', #126569 ) ;
#49305=FACE_OUTER_BOUND ( 'NONE', #46783, .T. ) ;
#49306=ORIENTED_EDGE ( 'NONE', *, *, #90459, .F. ) ;
#49307=DIRECTION ( 'NONE',  ( 0.7071067811865487940, -0.7071067811865463515, 0.000000000000000000 ) ) ;
#49308=EDGE_CURVE ( 'NONE', #142848, #105496, #72267, .T. ) ;
#49309=AXIS2_PLACEMENT_3D ( 'NONE', #126642, #7719, #138984 ) ;
#49310=DIRECTION ( 'NONE',  ( -0.000000000000000000, 0.000000000000000000, 1.000000000000000000 ) ) ;
#49311=DIRECTION ( 'NONE',  ( 0.7071067811865487940, 0.7071067811865463515, 0.000000000000000000 ) ) ;
#49312=ORIENTED_EDGE ( 'NONE', *, *, #101954, .T. ) ;
#49313=ORIENTED_EDGE ( 'NONE', *, *, #94602, .T. ) ;
#49314=VERTEX_POINT ( 'NONE', #104093 ) ;
#49315=CARTESIAN_POINT ( 'NONE',  ( 6.183988606268994381, 28.73617430169791476, 5.000000000000000000 ) ) ;
#49316=DIRECTION ( 'NONE',  ( 0.6830127018922180770, -0.6830127018922204085, -0.2588190451025213501 ) ) ;
#49318=VECTOR ( 'NONE', #39093, 1000.000000000000000 ) ;
#49321=DIRECTION ( 'NONE',  ( -0.7071067811865486830, -0.7071067811865464625, 0.000000000000000000 ) ) ;
#49322=EDGE_LOOP ( 'NONE', ( #110185, #55486, #108851 ) ) ;
#49323=ORIENTED_EDGE ( 'NONE', *, *, #32197, .T. ) ;
#49324=DIRECTION ( 'NONE',  ( 0.6830127018922181881, 0.6830127018922202975, -0.2588190451025214056 ) ) ;
#49325=EDGE_CURVE ( 'NONE', #110453, #3179, #17120, .T. ) ;
#49326=VERTEX_POINT ( 'NONE', #38174 ) ;
#49327=ORIENTED_EDGE ( 'NONE', *, *, #20192, .T. ) ;
#49328=VECTOR ( 'NONE', #125524, 1000.000000000000000 ) ;
#49329=VECTOR ( 'NONE', #3678, 1000.000000000000000 ) ;
#49330=CARTESIAN_POINT ( 'NONE',  ( 24.70710678118637915, 14.25929247661557220, 5.000000000000000000 ) ) ;
#49331=VECTOR ( 'NONE', #27744, 1000.000000000000000 ) ;
#49332=DIRECTION ( 'NONE',  ( -0.6830127018922181881, 0.6830127018922202975, -0.2588190451025214056 ) ) ;
#49333=PLANE ( 'NONE',  #137521 ) ;
#49334=ORIENTED_EDGE ( 'NONE', *, *, #47415, .T. ) ;
#49336=ADVANCED_FACE ( 'NONE', ( #80960 ), #25849, .F. ) ;
#49337=VECTOR ( 'NONE', #14750, 1000.000000000000000 ) ;
#49338=LINE ( 'NONE', #50734, #36371 ) ;
#49339=VECTOR ( 'NONE', #128767, 1000.000000000000000 ) ;
#49341=CARTESIAN_POINT ( 'NONE',  ( 23.51078643762690490, -27.52281430457038880, 5.000000000000000000 ) ) ;
#49342=FACE_OUTER_BOUND ( 'NONE', #102137, .T. ) ;
#49343=ORIENTED_EDGE ( 'NONE', *, *, #76673, .T. ) ;
#49344=CARTESIAN_POINT ( 'NONE',  ( 32.99999999999976552, -16.02097659208068947, -11.96015758381216365 ) ) ;
#49345=FACE_BOUND ( 'NONE', #27159, .T. ) ;
#49346=ORIENTED_EDGE ( 'NONE', *, *, #26359, .T. ) ;
#49347=DIRECTION ( 'NONE',  ( -0.3543493200069162685, -0.000000000000000000, -0.9351131265310288487 ) ) ;
#49348=LINE ( 'NONE', #72544, #68925 ) ;
#49349=EDGE_CURVE ( 'NONE', #58607, #9195, #60673, .T. ) ;
#49350=DIRECTION ( 'NONE',  ( -0.6830127018922181881, 0.6830127018922202975, -0.2588190451025214056 ) ) ;
#49351=ORIENTED_EDGE ( 'NONE', *, *, #12263, .T. ) ;
#49352=LINE ( 'NONE', #114556, #80607 ) ;
#49353=ORIENTED_EDGE ( 'NONE', *, *, #68289, .F. ) ;
#49354=VERTEX_POINT ( 'NONE', #49052 ) ;
#49355=ORIENTED_EDGE ( 'NONE', *, *, #22497, .F. ) ;
#49357=ORIENTED_EDGE ( 'NONE', *, *, #141716, .T. ) ;
#49358=VECTOR ( 'NONE', #18150, 1000.000000000000000 ) ;
#49359=DIRECTION ( 'NONE',  ( -0.7071067811865486830, 0.7071067811865464625, 0.000000000000000000 ) ) ;
#49360=DIRECTION ( 'NONE',  ( -0.7071067811865486830, -0.7071067811865464625, 0.000000000000000000 ) ) ;
#49362=ORIENTED_EDGE ( 'NONE', *, *, #133025, .F. ) ;
#49364=DIRECTION ( 'NONE',  ( -0.6830127018922180770, -0.6830127018922204085, -0.2588190451025213501 ) ) ;
#49365=AXIS2_PLACEMENT_3D ( 'NONE', #85334, #27380, #63636 ) ;
#49366=PLANE ( 'NONE',  #11240 ) ;
#49367=PLANE ( 'NONE',  #94866 ) ;
#49368=ADVANCED_FACE ( 'NONE', ( #93247 ), #41729, .T. ) ;
#49369=DIRECTION ( 'NONE',  ( 0.6830127018922181881, 0.6830127018922202975, -0.2588190451025214056 ) ) ;
#49370=VECTOR ( 'NONE', #37979, 1000.000000000000000 ) ;
#49371=DIRECTION ( 'NONE',  ( 0.3543493200069162685, -0.000000000000000000, -0.9351131265310288487 ) ) ;
#49373=ORIENTED_EDGE ( 'NONE', *, *, #120943, .T. ) ;
#49374=ORIENTED_EDGE ( 'NONE', *, *, #24015, .F. ) ;
#49376=DIRECTION ( 'NONE',  ( -0.000000000000000000, 0.000000000000000000, 1.000000000000000000 ) ) ;
#49377=VERTEX_POINT ( 'NONE', #109111 ) ;
#49378=ORIENTED_EDGE ( 'NONE', *, *, #137551, .F. ) ;
#49379=CARTESIAN_POINT ( 'NONE',  ( 60.48921356237309510, -27.52281430457097500, 5.000000000000000000 ) ) ;
#49381=EDGE_CURVE ( 'NONE', #108960, #86507, #46490, .T. ) ;
#49382=EDGE_CURVE ( 'NONE', #75689, #18121, #31573, .T. ) ;
#49384=VERTEX_POINT ( 'NONE', #96769 ) ;
#49386=ORIENTED_EDGE ( 'NONE', *, *, #51859, .T. ) ;
#49388=CARTESIAN_POINT ( 'NONE',  ( -25.49999999999981881, 13.08746187583910725, 4.000000000000000000 ) ) ;
#49389=VECTOR ( 'NONE', #70475, 1000.000000000000000 ) ;
#49390=CARTESIAN_POINT ( 'NONE',  ( 29.99999999999978328, -22.22500000000000142, 4.412002311790018894 ) ) ;
#49391=VECTOR ( 'NONE', #115651, 1000.000000000000000 ) ;
#49393=EDGE_LOOP ( 'NONE', ( #92523, #69683, #57763, #12108 ) ) ;
#49395=DIRECTION ( 'NONE',  ( -0.000000000000000000, -0.3543493200069152693, 0.9351131265310292928 ) ) ;
#49396=CARTESIAN_POINT ( 'NONE',  ( -34.42500000000001137, -3.022814304570547783, 5.000000000000000000 ) ) ;
#49397=ORIENTED_EDGE ( 'NONE', *, *, #67079, .F. ) ;
#49398=VERTEX_POINT ( 'NONE', #41012 ) ;
#49399=LINE ( 'NONE', #103032, #12489 ) ;
#49400=VERTEX_POINT ( 'NONE', #75796 ) ;
#49402=VECTOR ( 'NONE', #137704, 1000.000000000000000 ) ;
#49403=LINE ( 'NONE', #25451, #13871 ) ;
#49404=PLANE ( 'NONE',  #52042 ) ;
#49405=CARTESIAN_POINT ( 'NONE',  ( -11.99999999999992717, 11.58746187583913390, 4.000000000000000000 ) ) ;
#49408=ORIENTED_EDGE ( 'NONE', *, *, #39267, .F. ) ;
#49409=LINE ( 'NONE', #60273, #59882 ) ;
#49410=DIRECTION ( 'NONE',  ( -0.7071067811865487940, 0.7071067811865463515, -0.000000000000000000 ) ) ;
#49411=LINE ( 'NONE', #3683, #30330 ) ;
#49413=FACE_OUTER_BOUND ( 'NONE', #47123, .T. ) ;
#49414=VECTOR ( 'NONE', #4647, 999.9999999999998863 ) ;
#49415=DIRECTION ( 'NONE',  ( -0.7071067811865486830, 0.7071067811865464625, 0.000000000000000000 ) ) ;
#49416=ORIENTED_EDGE ( 'NONE', *, *, #84258, .F. ) ;
#49418=ORIENTED_EDGE ( 'NONE', *, *, #83488, .T. ) ;
#49419=VERTEX_POINT ( 'NONE', #141024 ) ;
#49422=VERTEX_POINT ( 'NONE', #42474 ) ;
#49423=LINE ( 'NONE', #16002, #134499 ) ;
#49424=CARTESIAN_POINT ( 'NONE',  ( -15.18398860626900237, 28.73617430169797871, 5.000000000000000000 ) ) ;
#49426=EDGE_LOOP ( 'NONE', ( #106818, #81080, #28824, #125946 ) ) ;
#49427=LINE ( 'NONE', #137848, #62416 ) ;
#49428=EDGE_CURVE ( 'NONE', #102574, #101765, #58727, .T. ) ;
#49429=DIRECTION ( 'NONE',  ( -0.000000000000000000, 0.000000000000000000, 1.000000000000000000 ) ) ;
#49431=DIRECTION ( 'NONE',  ( 0.7071067811865486830, -0.7071067811865463515, 0.000000000000000000 ) ) ;
#49432=DIRECTION ( 'NONE',  ( 1.000000000000000000, 0.000000000000000000, 0.000000000000000000 ) ) ;
#49435=CARTESIAN_POINT ( 'NONE',  ( 2.292893218813441880, -0.7407075233842735917, 5.000000000000000000 ) ) ;
#49437=LINE ( 'NONE', #16017, #57044 ) ;
#49438=EDGE_CURVE ( 'NONE', #133821, #42793, #54763, .T. ) ;
#49439=ORIENTED_EDGE ( 'NONE', *, *, #54373, .T. ) ;
#49440=EDGE_CURVE ( 'NONE', #127203, #120495, #131597, .T. ) ;
#49443=EDGE_LOOP ( 'NONE', ( #64244, #139631, #66155, #15877 ) ) ;
#49445=EDGE_LOOP ( 'NONE', ( #36123, #83620, #96954, #29192 ) ) ;
#49446=ORIENTED_EDGE ( 'NONE', *, *, #54470, .T. ) ;
#49447=VERTEX_POINT ( 'NONE', #30871 ) ;
#49448=VECTOR ( 'NONE', #40046, 1000.000000000000000 ) ;
#49449=DIRECTION ( 'NONE',  ( 0.7071067811865487940, 0.7071067811865463515, 0.000000000000000000 ) ) ;
#49450=DIRECTION ( 'NONE',  ( 0.7071067811865486830, -0.7071067811865464625, -0.000000000000000000 ) ) ;
#49451=VERTEX_POINT ( 'NONE', #97517 ) ;
#49452=LINE ( 'NONE', #40001, #138883 ) ;
#49453=DIRECTION ( 'NONE',  ( -0.7071067811865486830, -0.7071067811865464625, 0.000000000000000000 ) ) ;
#49454=EDGE_CURVE ( 'NONE', #108744, #117764, #141775, .T. ) ;
#49455=DIRECTION ( 'NONE',  ( 0.6830127018922180770, -0.6830127018922204085, -0.2588190451025213501 ) ) ;
#49457=ORIENTED_EDGE ( 'NONE', *, *, #108593, .T. ) ;
#49458=EDGE_CURVE ( 'NONE', #45672, #115183, #32289, .T. ) ;
#49459=CARTESIAN_POINT ( 'NONE',  ( -7.499999999999944045, 8.319652575858382804, -8.582050562765845214 ) ) ;
#49460=CARTESIAN_POINT ( 'NONE',  ( 4.213219033033557714, 12.75929247661559351, 10.29404684609036202 ) ) ;
#49463=DIRECTION ( 'NONE',  ( -0.7071067811865487940, 0.7071067811865463515, 0.000000000000000000 ) ) ;
#49465=DIRECTION ( 'NONE',  ( -0.000000000000000000, 0.000000000000000000, 1.000000000000000000 ) ) ;
#49468=EDGE_CURVE ( 'NONE', #118451, #63434, #118561, .T. ) ;
#49469=CARTESIAN_POINT ( 'NONE',  ( -2.510786437626908008, -27.52281430457053446, 5.000000000000000000 ) ) ;
#49470=VECTOR ( 'NONE', #59422, 1000.000000000000000 ) ;
#49472=VERTEX_POINT ( 'NONE', #98943 ) ;
#49474=EDGE_LOOP ( 'NONE', ( #34354, #29733, #115722, #66585 ) ) ;
#49475=FACE_OUTER_BOUND ( 'NONE', #115288, .T. ) ;
#49476=CARTESIAN_POINT ( 'NONE',  ( 9.707106781186476852, 5.259292476615659240, 5.000000000000000000 ) ) ;
#49478=EDGE_CURVE ( 'NONE', #85990, #27559, #119268, .T. ) ;
#49479=DIRECTION ( 'NONE',  ( -0.000000000000000000, 0.000000000000000000, 1.000000000000000000 ) ) ;
#49480=VECTOR ( 'NONE', #51142, 1000.000000000000000 ) ;
#49481=FACE_OUTER_BOUND ( 'NONE', #8090, .T. ) ;
#49482=FACE_OUTER_BOUND ( 'NONE', #57915, .T. ) ;
#49483=LINE ( 'NONE', #30558, #55747 ) ;
#49485=AXIS2_PLACEMENT_3D ( 'NONE', #24679, #92786, #26122 ) ;
#49486=ORIENTED_EDGE ( 'NONE', *, *, #34008, .T. ) ;
#49487=CARTESIAN_POINT ( 'NONE',  ( -45.29974487139158867, -27.71228299555237840, 4.000000000000000000 ) ) ;
#49489=ADVANCED_FACE ( 'NONE', ( #84539 ), #29410, .T. ) ;
#49490=CARTESIAN_POINT ( 'NONE',  ( 16.49999999999989342, 9.052185695429077583, 5.000000000000000000 ) ) ;
#49491=DIRECTION ( 'NONE',  ( 0.6830127018922181881, 0.6830127018922202975, -0.2588190451025214056 ) ) ;
#49492=DIRECTION ( 'NONE',  ( -4.681814790819591790E-17, -0.3543493200069152693, 0.9351131265310292928 ) ) ;
#49493=VECTOR ( 'NONE', #30403, 1000.000000000000000 ) ;
#49495=ORIENTED_EDGE ( 'NONE', *, *, #122883, .F. ) ;
#49497=EDGE_LOOP ( 'NONE', ( #86709, #27485, #115019, #138301 ) ) ;
#49498=CARTESIAN_POINT ( 'NONE',  ( 0.000000000000000000, 0.000000000000000000, 5.000000000000000000 ) ) ;
#49499=FACE_OUTER_BOUND ( 'NONE', #35843, .T. ) ;
#49500=CARTESIAN_POINT ( 'NONE',  ( -19.36246187583889977, 22.22499999999999432, 4.000000000000000000 ) ) ;
#49501=ADVANCED_FACE ( 'NONE', ( #96090 ), #140327, .F. ) ;
#49503=DIRECTION ( 'NONE',  ( 0.3543493200069162685, -0.000000000000000000, -0.9351131265310288487 ) ) ;
#49505=EDGE_CURVE ( 'NONE', #80353, #36162, #1740, .T. ) ;
#49506=AXIS2_PLACEMENT_3D ( 'NONE', #36331, #25425, #137793 ) ;
#49508=VERTEX_POINT ( 'NONE', #56918 ) ;
#49509=CARTESIAN_POINT ( 'NONE',  ( 13.49999999999990763, 11.52377502935404330, -1.522421517564115145 ) ) ;
#49510=CARTESIAN_POINT ( 'NONE',  ( -22.01987774928535657, -17.24070752338410983, 20.23474786156464233 ) ) ;
#49511=EDGE_LOOP ( 'NONE', ( #142058, #112300, #103971 ) ) ;
#49512=VERTEX_POINT ( 'NONE', #110523 ) ;
#49514=CARTESIAN_POINT ( 'NONE',  ( 19.05000000000000071, 3.174999999999997158, 4.000000000000000000 ) ) ;
#49515=ORIENTED_EDGE ( 'NONE', *, *, #119278, .F. ) ;
#49516=LINE ( 'NONE', #126318, #23671 ) ;
#49517=VERTEX_POINT ( 'NONE', #12651 ) ;
#49518=DIRECTION ( 'NONE',  ( -0.7071067811865486830, -0.7071067811865464625, 0.000000000000000000 ) ) ;
#49519=VECTOR ( 'NONE', #73614, 1000.000000000000000 ) ;
#49520=FACE_BOUND ( 'NONE', #77303, .T. ) ;
#49521=DIRECTION ( 'NONE',  ( -0.7071067811865487940, 0.7071067811865463515, -0.000000000000000000 ) ) ;
#49522=FACE_OUTER_BOUND ( 'NONE', #12195, .T. ) ;
#49523=ORIENTED_EDGE ( 'NONE', *, *, #133337, .F. ) ;
#49525=CARTESIAN_POINT ( 'NONE',  ( 26.67183060077628554, 11.25929247661559884, 4.000000000000000000 ) ) ;
#49526=ORIENTED_EDGE ( 'NONE', *, *, #22336, .F. ) ;
#49527=ORIENTED_EDGE ( 'NONE', *, *, #69893, .F. ) ;
#49528=CARTESIAN_POINT ( 'NONE',  ( 13.49999999999990585, 21.05218569542895679, 5.000000000000000000 ) ) ;
#49529=ORIENTED_EDGE ( 'NONE', *, *, #123186, .T. ) ;
#49530=VERTEX_POINT ( 'NONE', #24946 ) ;
#49532=AXIS2_PLACEMENT_3D ( 'NONE', #29521, #93371, #7024 ) ;
#49533=ORIENTED_EDGE ( 'NONE', *, *, #131670, .T. ) ;
#49534=FACE_OUTER_BOUND ( 'NONE', #117792, .T. ) ;
#49535=PLANE ( 'NONE',  #82037 ) ;
#49537=ORIENTED_EDGE ( 'NONE', *, *, #2716, .F. ) ;
#49538=VECTOR ( 'NONE', #104188, 1000.000000000000000 ) ;
#49539=CARTESIAN_POINT ( 'NONE',  ( -21.05633424050521540, 8.797022467481218300, 4.404357971607193889 ) ) ;
#49540=DIRECTION ( 'NONE',  ( -0.7071067811865486830, 0.7071067811865464625, 0.000000000000000000 ) ) ;
#49541=CARTESIAN_POINT ( 'NONE',  ( 33.18398860626899705, 28.73617430169810305, 5.000000000000000000 ) ) ;
#49544=VERTEX_POINT ( 'NONE', #33032 ) ;
#49545=VERTEX_POINT ( 'NONE', #77248 ) ;
#49546=CARTESIAN_POINT ( 'NONE',  ( 29.99999999999979750, 10.55218569542906515, 5.000000000000000000 ) ) ;
#49547=LINE ( 'NONE', #114742, #127652 ) ;
#49549=EDGE_LOOP ( 'NONE', ( #2419, #105975, #1572, #131684 ) ) ;
#49550=ORIENTED_EDGE ( 'NONE', *, *, #24860, .F. ) ;
#49551=FACE_OUTER_BOUND ( 'NONE', #74101, .T. ) ;
#49552=PLANE ( 'NONE',  #59129 ) ;
#49553=EDGE_CURVE ( 'NONE', #32782, #89832, #54047, .T. ) ;
#49554=EDGE_CURVE ( 'NONE', #54652, #131882, #11193, .T. ) ;
#49555=CARTESIAN_POINT ( 'NONE',  ( 11.29289321881337749, 2.259292476615696099, 5.000000000000000000 ) ) ;
#49556=ORIENTED_EDGE ( 'NONE', *, *, #1643, .F. ) ;
#49557=DIRECTION ( 'NONE',  ( -0.3543493200069162685, -0.000000000000000000, -0.9351131265310288487 ) ) ;
#49559=DIRECTION ( 'NONE',  ( -0.6830127018922181881, 0.6830127018922202975, -0.2588190451025214056 ) ) ;
#49560=VECTOR ( 'NONE', #143022, 999.9999999999998863 ) ;
#49562=LINE ( 'NONE', #37955, #125981 ) ;
#49563=ORIENTED_EDGE ( 'NONE', *, *, #26301, .T. ) ;
#49565=FACE_OUTER_BOUND ( 'NONE', #104006, .T. ) ;
#49566=DIRECTION ( 'NONE',  ( 0.3543493200069162685, -0.000000000000000000, -0.9351131265310288487 ) ) ;
#49567=DIRECTION ( 'NONE',  ( -0.000000000000000000, 0.000000000000000000, 1.000000000000000000 ) ) ;
#49568=DIRECTION ( 'NONE',  ( -0.000000000000000000, 0.000000000000000000, 1.000000000000000000 ) ) ;
#49569=ORIENTED_EDGE ( 'NONE', *, *, #126307, .F. ) ;
#49571=ORIENTED_EDGE ( 'NONE', *, *, #70576, .T. ) ;
#49572=CARTESIAN_POINT ( 'NONE',  ( 2.671830600776449405, -9.740707523384187994, 4.000000000000000000 ) ) ;
#49573=CARTESIAN_POINT ( 'NONE',  ( 5.999999999999967137, -13.44781430457069327, 5.000000000000000000 ) ) ;
#49574=DIRECTION ( 'NONE',  ( -0.3543493200069162685, -0.000000000000000000, -0.9351131265310288487 ) ) ;
#49577=VECTOR ( 'NONE', #61698, 999.9999999999998863 ) ;
#49578=FACE_OUTER_BOUND ( 'NONE', #61816, .T. ) ;
#49579=CARTESIAN_POINT ( 'NONE',  ( -63.48921356237309510, -27.52281430457099631, 5.000000000000000000 ) ) ;
#49580=CARTESIAN_POINT ( 'NONE',  ( -9.489213562373095101, -27.52281430457062328, 5.000000000000000000 ) ) ;
#49581=ORIENTED_EDGE ( 'NONE', *, *, #75575, .T. ) ;
#49582=ADVANCED_FACE ( 'NONE', ( #113386 ), #111998, .F. ) ;
#49583=FACE_OUTER_BOUND ( 'NONE', #84235, .T. ) ;
#49584=CARTESIAN_POINT ( 'NONE',  ( -32.99999999999976552, -19.06887692260762890, 4.000000000000000000 ) ) ;
#49586=AXIS2_PLACEMENT_3D ( 'NONE', #126837, #51455, #85470 ) ;
#49587=DIRECTION ( 'NONE',  ( 0.6830127018922180770, -0.6830127018922204085, -0.2588190451025213501 ) ) ;
#49590=ORIENTED_EDGE ( 'NONE', *, *, #18023, .F. ) ;
#49591=EDGE_LOOP ( 'NONE', ( #5125, #9760, #105924, #91995 ) ) ;
#49592=CARTESIAN_POINT ( 'NONE',  ( 34.42499999999998295, 0.000000000000000000, 4.500000000000000888 ) ) ;
#49593=FACE_OUTER_BOUND ( 'NONE', #96995, .T. ) ;
#49594=VECTOR ( 'NONE', #34717, 1000.000000000000227 ) ;
#49596=CARTESIAN_POINT ( 'NONE',  ( 31.49999999999978684, -2.947814304570800736, 5.000000000000000000 ) ) ;
#49598=CARTESIAN_POINT ( 'NONE',  ( 0.000000000000000000, 0.000000000000000000, 5.000000000000000000 ) ) ;
#49600=DIRECTION ( 'NONE',  ( 0.6830127018922181881, 0.6830127018922202975, -0.2588190451025214056 ) ) ;
#49601=ORIENTED_EDGE ( 'NONE', *, *, #50450, .F. ) ;
#49602=EDGE_CURVE ( 'NONE', #109637, #24531, #66354, .T. ) ;
#49603=DIRECTION ( 'NONE',  ( -0.3543493200069162685, -0.000000000000000000, -0.9351131265310288487 ) ) ;
#49604=LINE ( 'NONE', #3872, #2947 ) ;
#49606=DIRECTION ( 'NONE',  ( 0.7071067811865486830, -0.7071067811865464625, -0.000000000000000000 ) ) ;
#49609=CARTESIAN_POINT ( 'NONE',  ( -33.18398860626899705, 28.73617430169810305, 5.000000000000000000 ) ) ;
#49612=VECTOR ( 'NONE', #132267, 1000.000000000000000 ) ;
#49613=VERTEX_POINT ( 'NONE', #122855 ) ;
#49614=DIRECTION ( 'NONE',  ( 0.000000000000000000, 0.000000000000000000, 1.000000000000000000 ) ) ;
#49615=ORIENTED_EDGE ( 'NONE', *, *, #121071, .T. ) ;
#49617=AXIS2_PLACEMENT_3D ( 'NONE', #100011, #44219, #129224 ) ;
#49618=DIRECTION ( 'NONE',  ( 0.7071067811865486830, -0.7071067811865464625, -0.000000000000000000 ) ) ;
#49619=EDGE_CURVE ( 'NONE', #8014, #77672, #74009, .T. ) ;
#49620=FACE_OUTER_BOUND ( 'NONE', #7132, .T. ) ;
#49621=LINE ( 'NONE', #106065, #99805 ) ;
#49622=CARTESIAN_POINT ( 'NONE',  ( -13.49999999999990585, 9.052185695429077583, 5.000000000000000000 ) ) ;
#49623=EDGE_CURVE ( 'NONE', #57693, #71285, #41358, .T. ) ;
#49624=FACE_OUTER_BOUND ( 'NONE', #23072, .T. ) ;
#49626=ORIENTED_EDGE ( 'NONE', *, *, #114496, .F. ) ;
#49627=EDGE_CURVE ( 'NONE', #28687, #4133, #103921, .T. ) ;
#49628=FACE_OUTER_BOUND ( 'NONE', #122760, .T. ) ;
#49629=DIRECTION ( 'NONE',  ( -0.7071067811865486830, -0.7071067811865464625, 0.000000000000000000 ) ) ;
#49630=PLANE ( 'NONE',  #117267 ) ;
#49631=PLANE ( 'NONE',  #119160 ) ;
#49634=LINE ( 'NONE', #69971, #143409 ) ;
#49635=EDGE_LOOP ( 'NONE', ( #105852, #81989, #79323, #34304 ) ) ;
#49636=ORIENTED_EDGE ( 'NONE', *, *, #106212, .T. ) ;
#49638=EDGE_CURVE ( 'NONE', #70270, #59222, #103231, .T. ) ;
#49639=CARTESIAN_POINT ( 'NONE',  ( 0.000000000000000000, -21.72500000000000142, 4.500000000000000888 ) ) ;
#49641=DIRECTION ( 'NONE',  ( -0.3543493200069162685, -0.000000000000000000, -0.9351131265310288487 ) ) ;
#49642=VERTEX_POINT ( 'NONE', #52246 ) ;
#49643=ADVANCED_FACE ( 'NONE', ( #129085 ), #129803, .F. ) ;
#49645=CARTESIAN_POINT ( 'NONE',  ( 11.99451991528749417, 28.92564299267946382, 4.000000000000000000 ) ) ;
#49649=ORIENTED_EDGE ( 'NONE', *, *, #119738, .F. ) ;
#49650=ORIENTED_EDGE ( 'NONE', *, *, #129720, .F. ) ;
#49651=DIRECTION ( 'NONE',  ( -0.000000000000000000, -0.000000000000000000, 1.000000000000000000 ) ) ;
#49652=FACE_OUTER_BOUND ( 'NONE', #60417, .T. ) ;
#49653=PLANE ( 'NONE',  #109131 ) ;
#49654=DIRECTION ( 'NONE',  ( -0.7071067811865486830, -0.7071067811865464625, -0.000000000000000000 ) ) ;
#49655=DIRECTION ( 'NONE',  ( 0.7071067811865486830, -0.7071067811865464625, -0.000000000000000000 ) ) ;
#49657=ORIENTED_EDGE ( 'NONE', *, *, #68045, .T. ) ;
#49659=DIRECTION ( 'NONE',  ( 0.6830127018922180770, -0.6830127018922204085, -0.2588190451025213501 ) ) ;
#49660=CARTESIAN_POINT ( 'NONE',  ( -17.51078643762690845, -27.52281430457043143, 5.000000000000000000 ) ) ;
#49661=VECTOR ( 'NONE', #64674, 1000.000000000000000 ) ;
#49662=CARTESIAN_POINT ( 'NONE',  ( 7.889826771117839144, -22.22500000000000142, 4.785647885939351198 ) ) ;
#49663=ADVANCED_FACE ( 'NONE', ( #62432 ), #18897, .F. ) ;
#49665=EDGE_CURVE ( 'NONE', #45698, #116876, #37279, .T. ) ;
#49667=ORIENTED_EDGE ( 'NONE', *, *, #63136, .T. ) ;
#49668=DIRECTION ( 'NONE',  ( -0.7071067811865487940, 0.7071067811865463515, 0.000000000000000000 ) ) ;
#49669=CARTESIAN_POINT ( 'NONE',  ( -12.18398860626900060, 28.73617430169795739, 5.000000000000000000 ) ) ;
#49670=FACE_OUTER_BOUND ( 'NONE', #136146, .T. ) ;
#49671=LINE ( 'NONE', #4632, #126513 ) ;
#49672=ORIENTED_EDGE ( 'NONE', *, *, #55691, .F. ) ;
#49673=VERTEX_POINT ( 'NONE', #128397 ) ;
#49674=DIRECTION ( 'NONE',  ( 1.000000000000000000, 0.000000000000000000, 0.000000000000000000 ) ) ;
#49675=CARTESIAN_POINT ( 'NONE',  ( -34.45011844616454511, 9.002304141593867826, 5.000000000000000888 ) ) ;
#49677=ORIENTED_EDGE ( 'NONE', *, *, #130652, .T. ) ;
#49678=PLANE ( 'NONE',  #127796 ) ;
#49679=EDGE_LOOP ( 'NONE', ( #82156, #86721, #28897, #66313 ) ) ;
#49680=LINE ( 'NONE', #61295, #117395 ) ;
#49681=LINE ( 'NONE', #94560, #142017 ) ;
#49683=FACE_BOUND ( 'NONE', #6999, .T. ) ;
#49684=FACE_OUTER_BOUND ( 'NONE', #29086, .T. ) ;
#49686=DIRECTION ( 'NONE',  ( -0.7071067811865486830, -0.7071067811865464625, -0.000000000000000000 ) ) ;
#49687=DIRECTION ( 'NONE',  ( -0.6830127018922181881, 0.6830127018922202975, -0.2588190451025214056 ) ) ;
#49690=LINE ( 'NONE', #104000, #127382 ) ;
#49693=AXIS2_PLACEMENT_3D ( 'NONE', #32805, #124079, #11703 ) ;
#49694=VECTOR ( 'NONE', #110841, 999.9999999999998863 ) ;
#49695=VERTEX_POINT ( 'NONE', #3879 ) ;
#49697=ORIENTED_EDGE ( 'NONE', *, *, #55282, .T. ) ;
#49698=PLANE ( 'NONE',  #72142 ) ;
#49699=EDGE_CURVE ( 'NONE', #97631, #89986, #29073, .T. ) ;
#49700=CARTESIAN_POINT ( 'NONE',  ( 23.99999999999983302, -21.41253812416053748, 4.000000000000000000 ) ) ;
#49701=VECTOR ( 'NONE', #133147, 1000.000000000000227 ) ;
#49702=CARTESIAN_POINT ( 'NONE',  ( -24.48921356237309510, -27.52281430457072631, 5.000000000000000000 ) ) ;
#49703=ORIENTED_EDGE ( 'NONE', *, *, #96467, .F. ) ;
#49704=CARTESIAN_POINT ( 'NONE',  ( 4.499999999999972466, -11.94781430457070925, 5.000000000000000000 ) ) ;
#49706=CARTESIAN_POINT ( 'NONE',  ( -72.18398860626899705, 28.73617430169837661, 5.000000000000000000 ) ) ;
#49707=DIRECTION ( 'NONE',  ( 0.3543493200069162685, -0.000000000000000000, -0.9351131265310288487 ) ) ;
#49708=CARTESIAN_POINT ( 'NONE',  ( 13.11547925347946908, 3.815643823912585386, 4.000000000000000000 ) ) ;
#49709=DIRECTION ( 'NONE',  ( -0.7071067811865487940, 0.7071067811865463515, -0.000000000000000000 ) ) ;
#49710=DIRECTION ( 'NONE',  ( -0.6830127018922181881, 0.6830127018922202975, -0.2588190451025214056 ) ) ;
#49711=CARTESIAN_POINT ( 'NONE',  ( -26.99999999999981881, 2.342191155542426628, -5.001666872980022660 ) ) ;
#49712=VERTEX_POINT ( 'NONE', #39983 ) ;
#49713=DIRECTION ( 'NONE',  ( -0.6830127018922180770, -0.6830127018922204085, -0.2588190451025213501 ) ) ;
#49714=CARTESIAN_POINT ( 'NONE',  ( 15.29974487139158867, -27.71228299555216879, 4.000000000000000000 ) ) ;
#49715=ADVANCED_FACE ( 'NONE', ( #40672 ), #139291, .F. ) ;
#49716=ORIENTED_EDGE ( 'NONE', *, *, #36466, .F. ) ;
#49717=VERTEX_POINT ( 'NONE', #84201 ) ;
#49718=ADVANCED_FACE ( 'NONE', ( #125730 ), #74744, .F. ) ;
#49719=ADVANCED_FACE ( 'NONE', ( #118925 ), #84876, .F. ) ;
#49720=ORIENTED_EDGE ( 'NONE', *, *, #141309, .F. ) ;
#49722=VERTEX_POINT ( 'NONE', #3200 ) ;
#49723=EDGE_CURVE ( 'NONE', #92832, #8140, #47490, .T. ) ;
#49724=EDGE_CURVE ( 'NONE', #80852, #32222, #124992, .T. ) ;
#49727=ORIENTED_EDGE ( 'NONE', *, *, #85923, .F. ) ;
#49729=CARTESIAN_POINT ( 'NONE',  ( 14.67183060077636725, -21.74070752338406720, 4.000000000000000000 ) ) ;
#49730=EDGE_LOOP ( 'NONE', ( #49743, #127015, #55780, #117215 ) ) ;
#49731=LINE ( 'NONE', #19907, #117 ) ;
#49733=CARTESIAN_POINT ( 'NONE',  ( 17.99999999999987566, -16.60178936734446964, 0.8616154019347914694 ) ) ;
#49734=ORIENTED_EDGE ( 'NONE', *, *, #14885, .F. ) ;
#49739=EDGE_CURVE ( 'NONE', #7006, #14902, #59761, .T. ) ;
#49741=CARTESIAN_POINT ( 'NONE',  ( 1.499999999999994449, 5.696342897626511359, -7.587980461218396755 ) ) ;
#49742=ORIENTED_EDGE ( 'NONE', *, *, #59547, .T. ) ;
#49743=ORIENTED_EDGE ( 'NONE', *, *, #75596, .T. ) ;
#49744=EDGE_LOOP ( 'NONE', ( #3808, #92471, #120229, #77743 ) ) ;
#49745=EDGE_LOOP ( 'NONE', ( #75273, #51244, #87329, #58382 ) ) ;
#49746=LINE ( 'NONE', #83807, #716 ) ;
#49747=EDGE_CURVE ( 'NONE', #23427, #50436, #92340, .T. ) ;
#49748=DIRECTION ( 'NONE',  ( -0.7071067811865487940, 0.7071067811865463515, 0.000000000000000000 ) ) ;
#49749=DIRECTION ( 'NONE',  ( 0.3543493200069162685, -0.000000000000000000, -0.9351131265310288487 ) ) ;
#49750=CARTESIAN_POINT ( 'NONE',  ( -48.48921356237309510, -27.52281430457089328, 5.000000000000000000 ) ) ;
#49751=ORIENTED_EDGE ( 'NONE', *, *, #26794, .T. ) ;
#49752=CARTESIAN_POINT ( 'NONE',  ( 23.51078643762690490, -27.52281430457038880, 5.000000000000000000 ) ) ;
#49753=VERTEX_POINT ( 'NONE', #11563 ) ;
#49754=EDGE_CURVE ( 'NONE', #31683, #141054, #701, .T. ) ;
#49755=PLANE ( 'NONE',  #33266 ) ;
#49757=PLANE ( 'NONE',  #108620 ) ;
#49758=FACE_OUTER_BOUND ( 'NONE', #82982, .T. ) ;
#49759=CARTESIAN_POINT ( 'NONE',  ( 33.29974487139158867, -27.71228299555229313, 4.000000000000000000 ) ) ;
#49760=( BOUNDED_CURVE ( )  B_SPLINE_CURVE ( 3, ( #134864, #89880, #34815, #123266 ),
 .UNSPECIFIED., .F., .T. ) 
 B_SPLINE_CURVE_WITH_KNOTS ( ( 4, 4 ),
 ( 5.143245962375949887, 6.645403452391246191 ),
 .UNSPECIFIED. ) 
 CURVE ( )  GEOMETRIC_REPRESENTATION_ITEM ( )  RATIONAL_B_SPLINE_CURVE ( ( 1.000000000000000000, 0.8206354192515208368, 0.8206354192515208368, 1.000000000000000000 ) ) 
 REPRESENTATION_ITEM ( '' )  );
#49762=VERTEX_POINT ( 'NONE', #54424 ) ;
#49766=VERTEX_POINT ( 'NONE', #108732 ) ;
#49767=DIRECTION ( 'NONE',  ( 0.7071067811865487940, 0.7071067811865463515, 0.000000000000000000 ) ) ;
#49768=CARTESIAN_POINT ( 'NONE',  ( -2.999999999999975575, -18.03360074219755660, 5.000000000000000000 ) ) ;
#49770=LINE ( 'NONE', #36032, #10300 ) ;
#49774=EDGE_CURVE ( 'NONE', #11133, #61053, #89172, .T. ) ;
#49777=DIRECTION ( 'NONE',  ( 0.6830127018922180770, -0.6830127018922204085, -0.2588190451025214056 ) ) ;
#49778=LINE ( 'NONE', #72265, #141400 ) ;
#49779=EDGE_CURVE ( 'NONE', #73748, #68933, #142139, .T. ) ;
#49780=DIRECTION ( 'NONE',  ( -0.7071067811865487940, 0.7071067811865463515, 0.000000000000000000 ) ) ;
#49781=ORIENTED_EDGE ( 'NONE', *, *, #134996, .F. ) ;
#49782=DIRECTION ( 'NONE',  ( -0.7071067811865487940, 0.7071067811865463515, 0.000000000000000000 ) ) ;
#49783=ORIENTED_EDGE ( 'NONE', *, *, #91721, .F. ) ;
#49784=ADVANCED_FACE ( 'NONE', ( #42824 ), #87023, .F. ) ;
#49785=CARTESIAN_POINT ( 'NONE',  ( -34.92500000000001137, 22.22500000000000142, 4.000000000000000000 ) ) ;
#49786=CARTESIAN_POINT ( 'NONE',  ( -5.207106781186503497, 15.75929247661555976, 5.000000000000000000 ) ) ;
#49787=ORIENTED_EDGE ( 'NONE', *, *, #45314, .T. ) ;
#49788=DIRECTION ( 'NONE',  ( -0.000000000000000000, 0.3543493200069153248, 0.9351131265310292928 ) ) ;
#49789=LINE ( 'NONE', #105542, #47248 ) ;
#49791=ORIENTED_EDGE ( 'NONE', *, *, #4006, .T. ) ;
#49793=VERTEX_POINT ( 'NONE', #132708 ) ;
#49794=CARTESIAN_POINT ( 'NONE',  ( -72.18398860626899705, 28.73617430169837661, 5.000000000000000000 ) ) ;
#49795=VECTOR ( 'NONE', #107366, 999.9999999999998863 ) ;
#49797=DIRECTION ( 'NONE',  ( -0.7071067811865487940, 0.7071067811865463515, -0.000000000000000000 ) ) ;
#49798=VECTOR ( 'NONE', #91609, 999.9999999999998863 ) ;
#49801=EDGE_LOOP ( 'NONE', ( #20979, #70193, #75415, #95591 ) ) ;
#49802=VECTOR ( 'NONE', #53593, 999.9999999999998863 ) ;
#49803=ADVANCED_FACE ( 'NONE', ( #42112 ), #43515, .F. ) ;
#49804=DIRECTION ( 'NONE',  ( -0.6830127018922180770, -0.6830127018922204085, -0.2588190451025213501 ) ) ;
#49805=LINE ( 'NONE', #92534, #6783 ) ;
#49808=PLANE ( 'NONE',  #21308 ) ;
#49809=ORIENTED_EDGE ( 'NONE', *, *, #100053, .T. ) ;
#49810=EDGE_CURVE ( 'NONE', #6090, #39522, #78297, .T. ) ;
#49812=ORIENTED_EDGE ( 'NONE', *, *, #127406, .T. ) ;
#49814=CARTESIAN_POINT ( 'NONE',  ( -27.18398860626900060, 28.73617430169806042, 5.000000000000000000 ) ) ;
#49815=CARTESIAN_POINT ( 'NONE',  ( 16.74845587132414693, -11.24070752338416490, 10.39518518046005369 ) ) ;
#49816=CARTESIAN_POINT ( 'NONE',  ( -26.99999999999980815, -0.03360074219773377668, 5.000000000000000000 ) ) ;
#49817=VERTEX_POINT ( 'NONE', #55118 ) ;
#49819=CARTESIAN_POINT ( 'NONE',  ( -5.999999999999963585, -10.77435723561695902, -9.972017380717215218 ) ) ;
#49820=ADVANCED_FACE ( 'NONE', ( #87735 ), #75442, .F. ) ;
#49821=DIRECTION ( 'NONE',  ( 0.7071067811865487940, 0.7071067811865463515, -0.000000000000000000 ) ) ;
#49822=CARTESIAN_POINT ( 'NONE',  ( 48.48921356237309510, -27.52281430457089328, 5.000000000000000000 ) ) ;
#49823=EDGE_CURVE ( 'NONE', #80281, #3445, #66703, .T. ) ;
#49824=PLANE ( 'NONE',  #114588 ) ;
#49825=EDGE_LOOP ( 'NONE', ( #32438, #121731, #69105, #53595 ) ) ;
#49826=LINE ( 'NONE', #83886, #90117 ) ;
#49827=CARTESIAN_POINT ( 'NONE',  ( -22.96641869250914070, 7.680402717527123890, 4.333886692633072357 ) ) ;
#49828=LINE ( 'NONE', #18557, #51674 ) ;
#49829=LINE ( 'NONE', #17174, #28456 ) ;
#49832=ORIENTED_EDGE ( 'NONE', *, *, #55648, .T. ) ;
#49834=ORIENTED_EDGE ( 'NONE', *, *, #39241, .T. ) ;
#49836=LINE ( 'NONE', #102775, #112808 ) ;
#49837=LINE ( 'NONE', #48376, #50391 ) ;
#49838=CARTESIAN_POINT ( 'NONE',  ( -53.99451991528749062, 28.92564299267975869, 4.000000000000000000 ) ) ;
#49839=ORIENTED_EDGE ( 'NONE', *, *, #1541, .F. ) ;
#49841=DIRECTION ( 'NONE',  ( 0.3543493200069162685, -0.000000000000000000, -0.9351131265310288487 ) ) ;
#49842=ADVANCED_FACE ( 'NONE', ( #98600 ), #97136, .F. ) ;
#49846=CARTESIAN_POINT ( 'NONE',  ( 26.99451991528749417, 28.92564299267956685, 4.000000000000000000 ) ) ;
#49847=ORIENTED_EDGE ( 'NONE', *, *, #2875, .F. ) ;
#49848=VERTEX_POINT ( 'NONE', #121064 ) ;
#49851=DIRECTION ( 'NONE',  ( -0.6830127018922181881, 0.6830127018922202975, -0.2588190451025214056 ) ) ;
#49852=CARTESIAN_POINT ( 'NONE',  ( 14.99451991528749595, 28.92564299267948513, 4.000000000000000000 ) ) ;
#49853=CARTESIAN_POINT ( 'NONE',  ( 24.32816939922335564, -15.74070752338411694, 4.000000000000000000 ) ) ;
#49855=DIRECTION ( 'NONE',  ( -0.7071067811865486830, 0.7071067811865464625, 0.000000000000000000 ) ) ;
#49857=ORIENTED_EDGE ( 'NONE', *, *, #52294, .T. ) ;
#49858=VERTEX_POINT ( 'NONE', #59424 ) ;
#49860=VERTEX_POINT ( 'NONE', #48510 ) ;
#49861=CARTESIAN_POINT ( 'NONE',  ( -38.99451991528749062, 28.92564299267965211, 4.000000000000000000 ) ) ;
#49862=EDGE_LOOP ( 'NONE', ( #140864, #32512, #129138, #26453 ) ) ;
#49863=AXIS2_PLACEMENT_3D ( 'NONE', #107328, #119607, #108013 ) ;
#49865=DIRECTION ( 'NONE',  ( 0.7071067811865487940, 0.7071067811865463515, 0.000000000000000000 ) ) ;
#49866=DIRECTION ( 'NONE',  ( -0.000000000000000000, 0.3543493200069152138, -0.9351131265310292928 ) ) ;
#49867=EDGE_CURVE ( 'NONE', #80017, #138017, #15143, .T. ) ;
#49869=CARTESIAN_POINT ( 'NONE',  ( 10.49999999999992539, -8.947814304570741228, 5.000000000000000000 ) ) ;
#49870=ORIENTED_EDGE ( 'NONE', *, *, #61794, .F. ) ;
#49872=CARTESIAN_POINT ( 'NONE',  ( -19.49999999999987210, -2.777013188829482893, 4.549262955118030582 ) ) ;
#49873=ORIENTED_EDGE ( 'NONE', *, *, #54657, .F. ) ;
#49874=CARTESIAN_POINT ( 'NONE',  ( -18.12147316337136260, -20.24070752338408141, 7.412974875817832654 ) ) ;
#49875=VERTEX_POINT ( 'NONE', #25316 ) ;
#49876=EDGE_CURVE ( 'NONE', #115809, #18442, #117895, .T. ) ;
#49877=VERTEX_POINT ( 'NONE', #92712 ) ;
#49878=ADVANCED_FACE ( 'NONE', ( #23917 ), #23158, .F. ) ;
#49879=DIRECTION ( 'NONE',  ( 0.6830127018922181881, 0.6830127018922202975, -0.2588190451025214056 ) ) ;
#49880=VERTEX_POINT ( 'NONE', #13708 ) ;
#49883=EDGE_LOOP ( 'NONE', ( #101923, #132608, #41299, #91491 ) ) ;
#49886=ADVANCED_FACE ( 'NONE', ( #81897 ), #81159, .T. ) ;
#49888=VECTOR ( 'NONE', #58033, 999.9999999999998863 ) ;
#49889=CARTESIAN_POINT ( 'NONE',  ( 8.999999999999941380, -6.412538124160696462, 4.000000000000000000 ) ) ;
#49890=EDGE_CURVE ( 'NONE', #19532, #25917, #134843, .T. ) ;
#49892=DIRECTION ( 'NONE',  ( 0.7071067811865487940, 0.7071067811865463515, 0.000000000000000000 ) ) ;
#49893=AXIS2_PLACEMENT_3D ( 'NONE', #27385, #92645, #136887 ) ;
#49894=EDGE_CURVE ( 'NONE', #133528, #22423, #92007, .T. ) ;
#49896=FACE_OUTER_BOUND ( 'NONE', #58634, .T. ) ;
#49898=EDGE_CURVE ( 'NONE', #108369, #135769, #67436, .T. ) ;
#49899=PLANE ( 'NONE',  #125724 ) ;
#49900=EDGE_CURVE ( 'NONE', #126702, #1467, #35538, .T. ) ;
#49901=ORIENTED_EDGE ( 'NONE', *, *, #73956, .F. ) ;
#49902=LINE ( 'NONE', #39742, #112852 ) ;
#49903=LINE ( 'NONE', #107100, #79926 ) ;
#49904=ORIENTED_EDGE ( 'NONE', *, *, #111270, .F. ) ;
#49905=ORIENTED_EDGE ( 'NONE', *, *, #58758, .F. ) ;
#49906=DIRECTION ( 'NONE',  ( 0.6830127018922181881, 0.6830127018922202975, -0.2588190451025214056 ) ) ;
#49907=EDGE_LOOP ( 'NONE', ( #34151, #90792, #52924, #28309 ) ) ;
#49908=FACE_OUTER_BOUND ( 'NONE', #63228, .T. ) ;
#49910=EDGE_CURVE ( 'NONE', #5604, #60822, #12303, .T. ) ;
#49913=VERTEX_POINT ( 'NONE', #34795 ) ;
#49915=ORIENTED_EDGE ( 'NONE', *, *, #100191, .T. ) ;
#49916=EDGE_CURVE ( 'NONE', #40999, #76459, #90600, .T. ) ;
#49919=PLANE ( 'NONE',  #122253 ) ;
#49921=ORIENTED_EDGE ( 'NONE', *, *, #37158, .T. ) ;
#49923=VERTEX_POINT ( 'NONE', #101455 ) ;
#49924=CARTESIAN_POINT ( 'NONE',  ( -19.17183060077633172, -8.240707523384193323, 4.000000000000000000 ) ) ;
#49926=FACE_OUTER_BOUND ( 'NONE', #69382, .T. ) ;
#49927=LINE ( 'NONE', #94106, #56635 ) ;
#49928=CARTESIAN_POINT ( 'NONE',  ( -28.49999999999979394, 19.46639925780206326, 5.000000000000000000 ) ) ;
#49929=CARTESIAN_POINT ( 'NONE',  ( 17.29387692260792164, 22.22500000000000142, 4.000000000000000000 ) ) ;
#49931=CARTESIAN_POINT ( 'NONE',  ( 6.096670641874017527, -2.240707523384260824, 15.26439735382753859 ) ) ;
#49932=CARTESIAN_POINT ( 'NONE',  ( 11.81601139373100651, 28.73617430169779041, 5.000000000000000000 ) ) ;
#49933=LINE ( 'NONE', #113741, #37271 ) ;
#49935=ORIENTED_EDGE ( 'NONE', *, *, #26910, .F. ) ;
#49938=EDGE_LOOP ( 'NONE', ( #91812, #64922, #77080, #10961 ) ) ;
#49939=EDGE_CURVE ( 'NONE', #124008, #52318, #95574, .T. ) ;
#49940=CARTESIAN_POINT ( 'NONE',  ( 1.499999999999988232, -16.53360074219757792, 5.000000000000000000 ) ) ;
#49942=ORIENTED_EDGE ( 'NONE', *, *, #62698, .F. ) ;
#49943=DIRECTION ( 'NONE',  ( -0.7071067811865486830, -0.7071067811865464625, 0.000000000000000000 ) ) ;
#49944=CARTESIAN_POINT ( 'NONE',  ( -2.803796552228843275, -22.22500000000000142, 17.17192473999973146 ) ) ;
#49945=ORIENTED_EDGE ( 'NONE', *, *, #10257, .T. ) ;
#49946=FACE_OUTER_BOUND ( 'NONE', #84476, .T. ) ;
#49947=ORIENTED_EDGE ( 'NONE', *, *, #101707, .F. ) ;
#49948=CARTESIAN_POINT ( 'NONE',  ( -22.82816939922337696, 15.75929247661555976, 4.000000000000000000 ) ) ;
#49951=DIRECTION ( 'NONE',  ( -0.7071067811865487940, 0.7071067811865463515, 0.000000000000000000 ) ) ;
#49952=CARTESIAN_POINT ( 'NONE',  ( 8.816011393731004731, 28.73617430169781173, 5.000000000000000000 ) ) ;
#49954=EDGE_CURVE ( 'NONE', #142188, #80902, #139836, .T. ) ;
#49955=LINE ( 'NONE', #136944, #113936 ) ;
#49961=DIRECTION ( 'NONE',  ( -0.000000000000000000, 0.3543493200069153248, 0.9351131265310292928 ) ) ;
#49962=DIRECTION ( 'NONE',  ( -0.7071067811865487940, 0.7071067811865463515, -0.000000000000000000 ) ) ;
#49963=EDGE_LOOP ( 'NONE', ( #118153, #67638, #135694, #65603 ) ) ;
#49969=EDGE_CURVE ( 'NONE', #64566, #123173, #16572, .T. ) ;
#49971=CARTESIAN_POINT ( 'NONE',  ( 21.18398860626899349, 28.73617430169802134, 5.000000000000000000 ) ) ;
#49972=DIRECTION ( 'NONE',  ( -0.6830127018922181881, 0.6830127018922202975, -0.2588190451025214056 ) ) ;
#49974=LINE ( 'NONE', #94157, #13937 ) ;
#49975=LINE ( 'NONE', #28214, #81161 ) ;
#49976=FACE_OUTER_BOUND ( 'NONE', #92553, .T. ) ;
#49977=CARTESIAN_POINT ( 'NONE',  ( -20.81601139373100295, 28.73617430169773002, 5.000000000000000000 ) ) ;
#49978=EDGE_CURVE ( 'NONE', #101548, #70961, #40507, .T. ) ;
#49979=FACE_OUTER_BOUND ( 'NONE', #70032, .T. ) ;
#49982=LINE ( 'NONE', #136979, #12789 ) ;
#49984=DIRECTION ( 'NONE',  ( -0.7071067811865486830, 0.7071067811865464625, 0.000000000000000000 ) ) ;
#49985=CARTESIAN_POINT ( 'NONE',  ( 15.48921356237309510, -27.52281430457066236, 5.000000000000000000 ) ) ;
#49987=EDGE_LOOP ( 'NONE', ( #135416, #1385, #33543, #142902 ) ) ;
#49988=ORIENTED_EDGE ( 'NONE', *, *, #74849, .T. ) ;
#49989=AXIS2_PLACEMENT_3D ( 'NONE', #84252, #49491, #84930 ) ;
#49991=EDGE_LOOP ( 'NONE', ( #127637, #110830, #24533, #79098 ) ) ;
#49994=VECTOR ( 'NONE', #116438, 1000.000000000000000 ) ;
#49996=ORIENTED_EDGE ( 'NONE', *, *, #126307, .T. ) ;
#49998=CARTESIAN_POINT ( 'NONE',  ( -20.67183060077632817, 11.25929247661560595, 4.000000000000000000 ) ) ;
#50001=EDGE_CURVE ( 'NONE', #34999, #3157, #71707, .T. ) ;
#50003=EDGE_LOOP ( 'NONE', ( #142148, #127281, #13721 ) ) ;
#50004=LINE ( 'NONE', #141262, #111413 ) ;
#50005=ORIENTED_EDGE ( 'NONE', *, *, #125806, .F. ) ;
#50006=DIRECTION ( 'NONE',  ( 0.6830127018922180770, -0.6830127018922204085, -0.2588190451025213501 ) ) ;
#50007=CARTESIAN_POINT ( 'NONE',  ( -53.99451991528749062, 28.92564299267975869, 4.000000000000000000 ) ) ;
#50008=CARTESIAN_POINT ( 'NONE',  ( 32.48334561358932149, 22.22500000000000142, 4.500000000000000888 ) ) ;
#50009=CARTESIAN_POINT ( 'NONE',  ( -38.99451991528749062, 28.92564299267965211, 4.000000000000000000 ) ) ;
#50010=ORIENTED_EDGE ( 'NONE', *, *, #61919, .F. ) ;
#50012=VERTEX_POINT ( 'NONE', #51377 ) ;
#50013=CARTESIAN_POINT ( 'NONE',  ( 9.793339364578407924, 21.75929247661549937, 4.998822639870711626 ) ) ;
#50015=DIRECTION ( 'NONE',  ( -0.7071067811865486830, -0.7071067811865464625, 0.000000000000000000 ) ) ;
#50017=CARTESIAN_POINT ( 'NONE',  ( -42.48921356237308800, -27.52281430457085065, 5.000000000000000000 ) ) ;
#50019=DIRECTION ( 'NONE',  ( -0.7071067811865486830, -0.7071067811865464625, -0.000000000000000000 ) ) ;
#50020=VERTEX_POINT ( 'NONE', #104290 ) ;
#50021=EDGE_LOOP ( 'NONE', ( #8664, #133479, #61771, #11907 ) ) ;
#50022=CARTESIAN_POINT ( 'NONE',  ( 1.056153167756417099, -22.22500000000000142, -8.634603981399813222 ) ) ;
#50023=ORIENTED_EDGE ( 'NONE', *, *, #115188, .F. ) ;
#50024=ORIENTED_EDGE ( 'NONE', *, *, #103297, .T. ) ;
#50026=PLANE ( 'NONE',  #23451 ) ;
#50027=CARTESIAN_POINT ( 'NONE',  ( -15.18398860626900237, 28.73617430169797871, 5.000000000000000000 ) ) ;
#50028=VERTEX_POINT ( 'NONE', #15827 ) ;
#50029=PLANE ( 'NONE',  #108465 ) ;
#50030=CARTESIAN_POINT ( 'NONE',  ( 21.18398860626899349, 28.73617430169802134, 5.000000000000000000 ) ) ;
#50031=CARTESIAN_POINT ( 'NONE',  ( -81.18398860626899705, 28.73617430169844056, 5.000000000000000000 ) ) ;
#50032=CARTESIAN_POINT ( 'NONE',  ( -32.99999999999977263, -21.03360074219752462, 5.000000000000000000 ) ) ;
#50033=VERTEX_POINT ( 'NONE', #137682 ) ;
#50034=DIRECTION ( 'NONE',  ( 0.7071067811865487940, 0.7071067811865463515, 0.000000000000000000 ) ) ;
#50035=FACE_BOUND ( 'NONE', #53364, .T. ) ;
#50036=ORIENTED_EDGE ( 'NONE', *, *, #109282, .F. ) ;
#50037=DIRECTION ( 'NONE',  ( 0.6830127018922180770, 0.6830127018922202975, -0.2588190451025213501 ) ) ;
#50039=CARTESIAN_POINT ( 'NONE',  ( 27.48921356237309155, -27.52281430457074762, 5.000000000000000000 ) ) ;
#50040=ORIENTED_EDGE ( 'NONE', *, *, #12188, .F. ) ;
#50042=ORIENTED_EDGE ( 'NONE', *, *, #64125, .F. ) ;
#50043=ORIENTED_EDGE ( 'NONE', *, *, #105187, .T. ) ;
#50044=ORIENTED_EDGE ( 'NONE', *, *, #75797, .F. ) ;
#50045=VECTOR ( 'NONE', #118094, 1000.000000000000000 ) ;
#50046=ADVANCED_FACE ( 'NONE', ( #115873 ), #28191, .F. ) ;
#50048=ORIENTED_EDGE ( 'NONE', *, *, #98093, .F. ) ;
#50049=DIRECTION ( 'NONE',  ( 1.000000000000000000, 0.000000000000000000, 0.000000000000000000 ) ) ;
#50050=EDGE_CURVE ( 'NONE', #101903, #120463, #39062, .T. ) ;
#50051=AXIS2_PLACEMENT_3D ( 'NONE', #64803, #31457, #128624 ) ;
#50052=DIRECTION ( 'NONE',  ( -0.000000000000000000, -0.3543493200069152693, 0.9351131265310292928 ) ) ;
#50053=CARTESIAN_POINT ( 'NONE',  ( -36.18398860626899705, 28.73617430169812437, 5.000000000000000000 ) ) ;
#50055=LINE ( 'NONE', #141321, #27415 ) ;
#50056=EDGE_CURVE ( 'NONE', #70215, #142853, #139103, .T. ) ;
#50057=CARTESIAN_POINT ( 'NONE',  ( 3.183988606268992161, 28.73617430169789699, 5.000000000000000000 ) ) ;
#50058=CARTESIAN_POINT ( 'NONE',  ( 2.510786437626908008, -27.52281430457053446, 5.000000000000000000 ) ) ;
#50059=DIRECTION ( 'NONE',  ( 1.000000000000000000, -0.000000000000000000, 0.000000000000000000 ) ) ;
#50060=LINE ( 'NONE', #83397, #124670 ) ;
#50064=VERTEX_POINT ( 'NONE', #38356 ) ;
#50066=EDGE_LOOP ( 'NONE', ( #54927, #140414, #142241, #106491 ) ) ;
#50067=VERTEX_POINT ( 'NONE', #82571 ) ;
#50070=ORIENTED_EDGE ( 'NONE', *, *, #31255, .F. ) ;
#50071=CARTESIAN_POINT ( 'NONE',  ( 34.49999999999975131, -14.56887692260766620, 4.000000000000000000 ) ) ;
#50073=EDGE_CURVE ( 'NONE', #125316, #142771, #94839, .T. ) ;
#50074=LINE ( 'NONE', #14573, #108782 ) ;
#50077=VERTEX_POINT ( 'NONE', #138376 ) ;
#50078=EDGE_CURVE ( 'NONE', #118345, #143096, #52082, .T. ) ;
#50079=AXIS2_PLACEMENT_3D ( 'NONE', #141644, #119151, #29289 ) ;
#50080=AXIS2_PLACEMENT_3D ( 'NONE', #71966, #127007, #47384 ) ;
#50081=LINE ( 'NONE', #62388, #134709 ) ;
#50082=LINE ( 'NONE', #94272, #123775 ) ;
#50083=VECTOR ( 'NONE', #1456, 1000.000000000000000 ) ;
#50084=EDGE_LOOP ( 'NONE', ( #36175, #5054, #139329 ) ) ;
#50086=CARTESIAN_POINT ( 'NONE',  ( 32.67183060077624646, -0.7407075233842753681, 4.000000000000000000 ) ) ;
#50088=CARTESIAN_POINT ( 'NONE',  ( 0.000000000000000000, 0.000000000000000000, 5.000000000000000000 ) ) ;
#50089=ORIENTED_EDGE ( 'NONE', *, *, #99676, .F. ) ;
#50090=EDGE_LOOP ( 'NONE', ( #39351, #138256, #114752, #81143 ) ) ;
#50091=PLANE ( 'NONE',  #63456 ) ;
#50092=ORIENTED_EDGE ( 'NONE', *, *, #7454, .F. ) ;
#50094=PLANE ( 'NONE',  #120440 ) ;
#50095=CARTESIAN_POINT ( 'NONE',  ( 32.29289321881323360, -3.740707523384246613, 5.000000000000000000 ) ) ;
#50097=ORIENTED_EDGE ( 'NONE', *, *, #116552, .F. ) ;
#50099=CARTESIAN_POINT ( 'NONE',  ( 9.005480084712511157, 28.92564299267931816, 4.000000000000000000 ) ) ;
#50100=FACE_OUTER_BOUND ( 'NONE', #113743, .T. ) ;
#50101=ADVANCED_FACE ( 'NONE', ( #71003 ), #127496, .F. ) ;
#50102=VERTEX_POINT ( 'NONE', #84031 ) ;
#50103=CARTESIAN_POINT ( 'NONE',  ( 21.18398860626899349, 28.73617430169802134, 5.000000000000000000 ) ) ;
#50104=LINE ( 'NONE', #85551, #86364 ) ;
#50105=VERTEX_POINT ( 'NONE', #28904 ) ;
#50106=DIRECTION ( 'NONE',  ( -0.3543493200069162685, -0.000000000000000000, -0.9351131265310288487 ) ) ;
#50107=EDGE_LOOP ( 'NONE', ( #73440, #48838, #20227, #60715 ) ) ;
#50108=ORIENTED_EDGE ( 'NONE', *, *, #24651, .F. ) ;
#50109=DIRECTION ( 'NONE',  ( 0.7071067811865487940, 0.7071067811865463515, 0.000000000000000000 ) ) ;
#50111=ORIENTED_EDGE ( 'NONE', *, *, #48877, .T. ) ;
#50112=CARTESIAN_POINT ( 'NONE',  ( 18.48921356237309510, -27.52281430457068367, 5.000000000000000000 ) ) ;
#50113=DIRECTION ( 'NONE',  ( 0.3543493200069162685, -0.000000000000000000, -0.9351131265310288487 ) ) ;
#50114=VECTOR ( 'NONE', #74691, 1000.000000000000227 ) ;
#50115=CARTESIAN_POINT ( 'NONE',  ( 24.32816939922336275, 17.25929247661554200, 4.000000000000000000 ) ) ;
#50117=LINE ( 'NONE', #105880, #92483 ) ;
#50118=DIRECTION ( 'NONE',  ( 0.7071067811865486830, -0.7071067811865464625, -0.000000000000000000 ) ) ;
#50119=EDGE_CURVE ( 'NONE', #47599, #116794, #110014, .T. ) ;
#50120=CARTESIAN_POINT ( 'NONE',  ( 51.29974487139158867, -27.71228299555242103, 4.000000000000000000 ) ) ;
#50121=DIRECTION ( 'NONE',  ( 0.3543493200069162685, -0.000000000000000000, -0.9351131265310288487 ) ) ;
#50122=CARTESIAN_POINT ( 'NONE',  ( -14.70025512860841133, -27.71228299555195917, 4.000000000000000000 ) ) ;
#50123=CARTESIAN_POINT ( 'NONE',  ( 0.000000000000000000, 0.000000000000000000, 5.000000000000000000 ) ) ;
#50124=AXIS2_PLACEMENT_3D ( 'NONE', #4068, #136071, #137516 ) ;
#50125=CARTESIAN_POINT ( 'NONE',  ( 21.16809626817622103, 8.755558144015518351, 4.000000000000000000 ) ) ;
#50127=VERTEX_POINT ( 'NONE', #20143 ) ;
#50128=ORIENTED_EDGE ( 'NONE', *, *, #21897, .F. ) ;
#50129=ORIENTED_EDGE ( 'NONE', *, *, #65507, .F. ) ;
#50131=EDGE_LOOP ( 'NONE', ( #3557, #95148, #16798, #128944 ) ) ;
#50132=EDGE_LOOP ( 'NONE', ( #3528, #139298, #83182, #82330 ) ) ;
#50133=EDGE_CURVE ( 'NONE', #78430, #27599, #96964, .T. ) ;
#50134=VERTEX_POINT ( 'NONE', #54259 ) ;
#50135=VECTOR ( 'NONE', #96092, 1000.000000000000227 ) ;
#50136=CARTESIAN_POINT ( 'NONE',  ( -42.48921356237308800, -27.52281430457085065, 5.000000000000000000 ) ) ;
#50137=DIRECTION ( 'NONE',  ( -0.7071067811865486830, -0.7071067811865464625, -0.000000000000000000 ) ) ;
#50138=ORIENTED_EDGE ( 'NONE', *, *, #135634, .F. ) ;
#50139=CARTESIAN_POINT ( 'NONE',  ( 10.49999999999992539, -13.53360074219760101, 5.000000000000000000 ) ) ;
#50140=CARTESIAN_POINT ( 'NONE',  ( -17.18753812416040461, -22.22500000000000142, 4.000000000000000000 ) ) ;
#50141=LINE ( 'NONE', #138575, #124969 ) ;
#50142=CARTESIAN_POINT ( 'NONE',  ( 21.18398860626899349, 28.73617430169802134, 5.000000000000000000 ) ) ;
#50144=EDGE_CURVE ( 'NONE', #68374, #76484, #108554, .T. ) ;
#50145=ORIENTED_EDGE ( 'NONE', *, *, #102624, .T. ) ;
#50146=ADVANCED_FACE ( 'NONE', ( #86862 ), #64383, .F. ) ;
#50147=CARTESIAN_POINT ( 'NONE',  ( -0.6614269816723958861, 22.22500000000000142, 17.98374865626361796 ) ) ;
#50149=CARTESIAN_POINT ( 'NONE',  ( -13.49999999999990408, -7.533600742197660516, 5.000000000000000000 ) ) ;
#50150=CARTESIAN_POINT ( 'NONE',  ( -47.99451991528749062, 28.92564299267971251, 4.000000000000000000 ) ) ;
#50151=FACE_OUTER_BOUND ( 'NONE', #62445, .T. ) ;
#50152=LINE ( 'NONE', #63198, #43062 ) ;
#50154=VECTOR ( 'NONE', #43798, 1000.000000000000000 ) ;
#50155=LINE ( 'NONE', #28400, #58406 ) ;
#50158=VERTEX_POINT ( 'NONE', #41931 ) ;
#50160=VECTOR ( 'NONE', #87619, 1000.000000000000000 ) ;
#50162=CARTESIAN_POINT ( 'NONE',  ( -1.171830600776460285, 21.75929247661549581, 4.000000000000000000 ) ) ;
#50165=DIRECTION ( 'NONE',  ( -0.6830127018922180770, -0.6830127018922204085, -0.2588190451025213501 ) ) ;
#50166=EDGE_CURVE ( 'NONE', #95429, #138852, #132795, .T. ) ;
#50167=LINE ( 'NONE', #7334, #37632 ) ;
#50169=CARTESIAN_POINT ( 'NONE',  ( 53.99451991528749062, 28.92564299267975869, 4.000000000000000000 ) ) ;
#50171=EDGE_CURVE ( 'NONE', #117371, #67034, #121601, .T. ) ;
#50173=EDGE_LOOP ( 'NONE', ( #133843, #6533, #128566, #83693 ) ) ;
#50176=CARTESIAN_POINT ( 'NONE',  ( -1.499999999999984013, -2.947814304570802513, 5.000000000000000000 ) ) ;
#50177=CARTESIAN_POINT ( 'NONE',  ( -11.70025512860841133, -27.71228299555198049, 4.000000000000000000 ) ) ;
#50179=DIRECTION ( 'NONE',  ( -0.7071067811865486830, 0.7071067811865464625, 0.000000000000000000 ) ) ;
#50180=EDGE_CURVE ( 'NONE', #29177, #30662, #75976, .T. ) ;
#50181=ORIENTED_EDGE ( 'NONE', *, *, #69811, .F. ) ;
#50184=ORIENTED_EDGE ( 'NONE', *, *, #3880, .T. ) ;
#50185=DIRECTION ( 'NONE',  ( 0.6830127018922181881, 0.6830127018922202975, -0.2588190451025214056 ) ) ;
#50186=EDGE_CURVE ( 'NONE', #23136, #92499, #66536, .T. ) ;
#50187=DIRECTION ( 'NONE',  ( 0.7071067811865487940, 0.7071067811865463515, 0.000000000000000000 ) ) ;
#50188=DIRECTION ( 'NONE',  ( 0.7071067811865487940, 0.7071067811865463515, 0.000000000000000000 ) ) ;
#50189=CARTESIAN_POINT ( 'NONE',  ( 5.999999999999961808, -6.033600742197678279, 5.000000000000000000 ) ) ;
#50191=VECTOR ( 'NONE', #15206, 1000.000000000000000 ) ;
#50192=VECTOR ( 'NONE', #137892, 999.9999999999998863 ) ;
#50194=ORIENTED_EDGE ( 'NONE', *, *, #10838, .T. ) ;
#50196=CARTESIAN_POINT ( 'NONE',  ( 34.47516574401890921, -4.509482387884330201, 4.998110765256834398 ) ) ;
#50197=EDGE_LOOP ( 'NONE', ( #42378, #79558, #4592, #90607 ) ) ;
#50198=EDGE_LOOP ( 'NONE', ( #14933, #51844, #67289, #89928, #116686 ) ) ;
#50199=VECTOR ( 'NONE', #62990, 1000.000000000000000 ) ;
#50200=DIRECTION ( 'NONE',  ( 0.7071067811865487940, 0.7071067811865463515, -0.000000000000000000 ) ) ;
#50201=ORIENTED_EDGE ( 'NONE', *, *, #22647, .F. ) ;
#50203=CARTESIAN_POINT ( 'NONE',  ( -78.48921356237309510, -27.52281430457109934, 5.000000000000000000 ) ) ;
#50205=VERTEX_POINT ( 'NONE', #10681 ) ;
#50206=LINE ( 'NONE', #116869, #54901 ) ;
#50207=FACE_OUTER_BOUND ( 'NONE', #54185, .T. ) ;
#50208=FACE_BOUND ( 'NONE', #103331, .T. ) ;
#50209=CARTESIAN_POINT ( 'NONE',  ( 9.005480084712511157, 28.92564299267931816, 4.000000000000000000 ) ) ;
#50210=LINE ( 'NONE', #103827, #49125 ) ;
#50211=CARTESIAN_POINT ( 'NONE',  ( -11.21837311707497165, 21.74787736706806385, 4.999607392498048419 ) ) ;
#50212=VERTEX_POINT ( 'NONE', #21598 ) ;
#50213=CARTESIAN_POINT ( 'NONE',  ( -13.36902924655238323, 1.333290112598358945, 4.303104124266152297 ) ) ;
#50214=CARTESIAN_POINT ( 'NONE',  ( -11.70025512860841133, -27.71228299555198049, 4.000000000000000000 ) ) ;
#50215=ORIENTED_EDGE ( 'NONE', *, *, #29273, .T. ) ;
#50216=EDGE_LOOP ( 'NONE', ( #68853, #55569, #115672, #133503 ) ) ;
#50217=LINE ( 'NONE', #8092, #14748 ) ;
#50218=VERTEX_POINT ( 'NONE', #120147 ) ;
#50220=ORIENTED_EDGE ( 'NONE', *, *, #102795, .T. ) ;
#50222=VECTOR ( 'NONE', #3842, 1000.000000000000000 ) ;
#50223=VERTEX_POINT ( 'NONE', #65124 ) ;
#50224=DIRECTION ( 'NONE',  ( -0.3543493200069162685, -0.000000000000000000, -0.9351131265310288487 ) ) ;
#50225=EDGE_CURVE ( 'NONE', #16867, #98425, #143363, .T. ) ;
#50226=DIRECTION ( 'NONE',  ( 0.7071067811865487940, 0.7071067811865463515, 0.000000000000000000 ) ) ;
#50228=AXIS2_PLACEMENT_3D ( 'NONE', #56629, #69622, #133434 ) ;
#50229=EDGE_CURVE ( 'NONE', #48577, #44804, #527, .T. ) ;
#50230=ADVANCED_FACE ( 'NONE', ( #118752 ), #88290, .F. ) ;
#50231=FACE_OUTER_BOUND ( 'NONE', #118696, .T. ) ;
#50232=CARTESIAN_POINT ( 'NONE',  ( 0.000000000000000000, 0.000000000000000000, 5.000000000000000000 ) ) ;
#50233=LINE ( 'NONE', #7401, #80605 ) ;
#50234=DIRECTION ( 'NONE',  ( -0.7071067811865487940, 0.7071067811865463515, -0.000000000000000000 ) ) ;
#50235=DIRECTION ( 'NONE',  ( -0.7071067811865486830, -0.7071067811865464625, 0.000000000000000000 ) ) ;
#50236=VERTEX_POINT ( 'NONE', #99864 ) ;
#50237=ORIENTED_EDGE ( 'NONE', *, *, #128471, .F. ) ;
#50238=LINE ( 'NONE', #114049, #95972 ) ;
#50239=DIRECTION ( 'NONE',  ( 0.7071067811865486830, -0.7071067811865464625, -0.000000000000000000 ) ) ;
#50240=VERTEX_POINT ( 'NONE', #87565 ) ;
#50241=ORIENTED_EDGE ( 'NONE', *, *, #29909, .F. ) ;
#50243=CARTESIAN_POINT ( 'NONE',  ( -0.1839886062690032631, 28.73617430169787568, 5.000000000000000000 ) ) ;
#50244=EDGE_CURVE ( 'NONE', #95686, #11445, #131790, .T. ) ;
#50245=VECTOR ( 'NONE', #45767, 999.9999999999998863 ) ;
#50246=EDGE_CURVE ( 'NONE', #33310, #78073, #85398, .T. ) ;
#50247=DIRECTION ( 'NONE',  ( 0.7071067811865486830, -0.7071067811865464625, -0.000000000000000000 ) ) ;
#50248=VERTEX_POINT ( 'NONE', #130370 ) ;
#50249=CARTESIAN_POINT ( 'NONE',  ( -13.17183060077637613, 18.75929247661552068, 4.000000000000000000 ) ) ;
#50250=EDGE_CURVE ( 'NONE', #126051, #133821, #31062, .T. ) ;
#50251=AXIS2_PLACEMENT_3D ( 'NONE', #34182, #112451, #100851 ) ;
#50252=DIRECTION ( 'NONE',  ( -1.000000000000000000, 0.000000000000000000, 0.000000000000000000 ) ) ;
#50254=LINE ( 'NONE', #137259, #63496 ) ;
#50255=EDGE_LOOP ( 'NONE', ( #17074, #120747, #126152, #65193 ) ) ;
#50257=CARTESIAN_POINT ( 'NONE',  ( 75.29974487139158157, -27.71228299555258445, 4.000000000000000000 ) ) ;
#50258=CARTESIAN_POINT ( 'NONE',  ( 45.18398860626900415, 28.73617430169818832, 5.000000000000000000 ) ) ;
#50259=EDGE_CURVE ( 'NONE', #128612, #83675, #102735, .T. ) ;
#50260=DIRECTION ( 'NONE',  ( 1.000000000000000000, 0.000000000000000000, 0.000000000000000000 ) ) ;
#50262=CARTESIAN_POINT ( 'NONE',  ( 39.48921356237310221, -27.52281430457082934, 5.000000000000000000 ) ) ;
#50263=ORIENTED_EDGE ( 'NONE', *, *, #75388, .F. ) ;
#50264=LINE ( 'NONE', #27060, #130617 ) ;
#50265=PLANE ( 'NONE',  #44698 ) ;
#50267=ORIENTED_EDGE ( 'NONE', *, *, #116546, .T. ) ;
#50268=CARTESIAN_POINT ( 'NONE',  ( -18.18398860626898994, 28.73617430169800002, 5.000000000000000000 ) ) ;
#50270=CARTESIAN_POINT ( 'NONE',  ( -34.92500000000001137, -6.183345613589518841, 4.500000000000000888 ) ) ;
#50271=ADVANCED_FACE ( 'NONE', ( #114307 ), #89700, .F. ) ;
#50272=VERTEX_POINT ( 'NONE', #68690 ) ;
#50273=PLANE ( 'NONE',  #39317 ) ;
#50274=DIRECTION ( 'NONE',  ( -0.7071067811865486830, -0.7071067811865464625, -0.000000000000000000 ) ) ;
#50275=CARTESIAN_POINT ( 'NONE',  ( 18.48921356237309510, -27.52281430457068367, 5.000000000000000000 ) ) ;
#50276=PLANE ( 'NONE',  #118982 ) ;
#50277=CARTESIAN_POINT ( 'NONE',  ( 12.81246187583938223, -22.22500000000000142, 4.000000000000000000 ) ) ;
#50278=ORIENTED_EDGE ( 'NONE', *, *, #138826, .F. ) ;
#50279=EDGE_CURVE ( 'NONE', #111091, #123707, #45522, .T. ) ;
#50282=FACE_OUTER_BOUND ( 'NONE', #43501, .T. ) ;
#50284=AXIS2_PLACEMENT_3D ( 'NONE', #55119, #129086, #32655 ) ;
#50285=VECTOR ( 'NONE', #99937, 1000.000000000000227 ) ;
#50288=CARTESIAN_POINT ( 'NONE',  ( 0.000000000000000000, 0.000000000000000000, 5.000000000000000000 ) ) ;
#50289=CARTESIAN_POINT ( 'NONE',  ( 17.20710678118642889, -5.240707523384228850, 5.000000000000000000 ) ) ;
#50290=CARTESIAN_POINT ( 'NONE',  ( -17.99999999999986855, -22.22500000000000142, 4.412002311790053533 ) ) ;
#50291=PLANE ( 'NONE',  #83899 ) ;
#50292=VERTEX_POINT ( 'NONE', #14984 ) ;
#50293=LINE ( 'NONE', #95918, #132164 ) ;
#50294=VECTOR ( 'NONE', #57850, 1000.000000000000227 ) ;
#50295=DIRECTION ( 'NONE',  ( -0.3543493200069162685, -0.000000000000000000, -0.9351131265310288487 ) ) ;
#50296=CARTESIAN_POINT ( 'NONE',  ( -33.29974487139158867, -27.71228299555229313, 4.000000000000000000 ) ) ;
#50297=VECTOR ( 'NONE', #68380, 1000.000000000000000 ) ;
#50298=PLANE ( 'NONE',  #106154 ) ;
#50300=DIRECTION ( 'NONE',  ( -0.6830127018922180770, -0.6830127018922204085, -0.2588190451025213501 ) ) ;
#50301=ORIENTED_EDGE ( 'NONE', *, *, #23637, .T. ) ;
#50302=EDGE_LOOP ( 'NONE', ( #36815, #85640, #83453, #68668 ) ) ;
#50303=ADVANCED_FACE ( 'NONE', ( #112189 ), #69398, .F. ) ;
#50305=PLANE ( 'NONE',  #103295 ) ;
#50306=DIRECTION ( 'NONE',  ( 0.7071067811865487940, 0.7071067811865463515, -0.000000000000000000 ) ) ;
#50308=FACE_OUTER_BOUND ( 'NONE', #15259, .T. ) ;
#50309=DIRECTION ( 'NONE',  ( -0.7071067811865486830, 0.7071067811865464625, 0.000000000000000000 ) ) ;
#50310=FACE_OUTER_BOUND ( 'NONE', #14441, .T. ) ;
#50311=EDGE_CURVE ( 'NONE', #98221, #8240, #91161, .T. ) ;
#50312=ORIENTED_EDGE ( 'NONE', *, *, #139650, .F. ) ;
#50313=PLANE ( 'NONE',  #58080 ) ;
#50314=CARTESIAN_POINT ( 'NONE',  ( -12.79289321881336328, 15.75929247661555443, 5.000000000000000000 ) ) ;
#50315=VECTOR ( 'NONE', #29708, 1000.000000000000000 ) ;
#50316=PLANE ( 'NONE',  #121933 ) ;
#50317=CARTESIAN_POINT ( 'NONE',  ( -66.48921356237309510, -27.52281430457101763, 5.000000000000000000 ) ) ;
#50318=DIRECTION ( 'NONE',  ( -0.000000000000000000, 0.000000000000000000, 1.000000000000000000 ) ) ;
#50320=AXIS2_PLACEMENT_3D ( 'NONE', #106753, #22149, #101150 ) ;
#50321=CARTESIAN_POINT ( 'NONE',  ( -59.99451991528749772, 28.92564299267980132, 4.000000000000000000 ) ) ;
#50322=ORIENTED_EDGE ( 'NONE', *, *, #136185, .T. ) ;
#50323=ORIENTED_EDGE ( 'NONE', *, *, #29816, .T. ) ;
#50325=LINE ( 'NONE', #95234, #42465 ) ;
#50326=CARTESIAN_POINT ( 'NONE',  ( -15.48921356237309510, -27.52281430457066236, 5.000000000000000000 ) ) ;
#50327=EDGE_CURVE ( 'NONE', #141201, #62928, #124474, .T. ) ;
#50328=VECTOR ( 'NONE', #101329, 1000.000000000000000 ) ;
#50329=ORIENTED_EDGE ( 'NONE', *, *, #76406, .T. ) ;
#50330=LINE ( 'NONE', #116993, #139380 ) ;
#50331=LINE ( 'NONE', #37311, #28179 ) ;
#50333=EDGE_CURVE ( 'NONE', #81104, #91540, #89016, .T. ) ;
#50334=AXIS2_PLACEMENT_3D ( 'NONE', #54271, #17991, #29605 ) ;
#50335=CARTESIAN_POINT ( 'NONE',  ( -42.29974487139158157, -27.71228299555235708, 4.000000000000000000 ) ) ;
#50336=ORIENTED_EDGE ( 'NONE', *, *, #94911, .T. ) ;
#50337=ORIENTED_EDGE ( 'NONE', *, *, #12896, .F. ) ;
#50339=DIRECTION ( 'NONE',  ( -0.7071067811865486830, -0.7071067811865464625, -0.000000000000000000 ) ) ;
#50340=DIRECTION ( 'NONE',  ( -0.7071067811865487940, 0.7071067811865463515, -0.000000000000000000 ) ) ;
#50342=EDGE_CURVE ( 'NONE', #134381, #129741, #34614, .T. ) ;
#50343=CARTESIAN_POINT ( 'NONE',  ( -21.18398860626899349, 28.73617430169802134, 5.000000000000000000 ) ) ;
#50346=EDGE_CURVE ( 'NONE', #128067, #82630, #103413, .T. ) ;
#50348=LINE ( 'NONE', #14843, #128808 ) ;
#50349=CARTESIAN_POINT ( 'NONE',  ( -6.707106781186496391, 2.259292476615697876, 5.000000000000000000 ) ) ;
#50350=DIRECTION ( 'NONE',  ( -0.3543493200069162685, -0.000000000000000000, -0.9351131265310288487 ) ) ;
#50351=ORIENTED_EDGE ( 'NONE', *, *, #41636, .F. ) ;
#50352=VERTEX_POINT ( 'NONE', #56413 ) ;
#50353=VECTOR ( 'NONE', #53788, 1000.000000000000000 ) ;
#50354=EDGE_CURVE ( 'NONE', #49384, #90110, #100596, .T. ) ;
#50355=DIRECTION ( 'NONE',  ( 0.6830127018922181881, 0.6830127018922202975, -0.2588190451025214056 ) ) ;
#50356=DIRECTION ( 'NONE',  ( -0.7071067811865487940, 0.7071067811865463515, 0.000000000000000000 ) ) ;
#50357=CARTESIAN_POINT ( 'NONE',  ( 9.183988606268997046, 28.73617430169793607, 5.000000000000000000 ) ) ;
#50358=VECTOR ( 'NONE', #131443, 1000.000000000000000 ) ;
#50360=CARTESIAN_POINT ( 'NONE',  ( 39.29974487139159578, -27.71228299555233576, 4.000000000000000000 ) ) ;
#50363=DIRECTION ( 'NONE',  ( 0.7071067811865487940, 0.7071067811865463515, 0.000000000000000000 ) ) ;
#50365=EDGE_LOOP ( 'NONE', ( #50145, #4847, #53634, #108625 ) ) ;
#50366=ADVANCED_FACE ( 'NONE', ( #44826 ), #78850, .F. ) ;
#50367=EDGE_LOOP ( 'NONE', ( #19215, #7679, #124407 ) ) ;
#50368=CARTESIAN_POINT ( 'NONE',  ( -42.48921356237308800, -27.52281430457085065, 5.000000000000000000 ) ) ;
#50369=ORIENTED_EDGE ( 'NONE', *, *, #76097, .F. ) ;
#50370=PLANE ( 'NONE',  #71092 ) ;
#50371=DIRECTION ( 'NONE',  ( -0.7071067811865486830, -0.7071067811865464625, 0.000000000000000000 ) ) ;
#50372=EDGE_CURVE ( 'NONE', #100169, #41854, #33912, .T. ) ;
#50373=AXIS2_PLACEMENT_3D ( 'NONE', #15763, #106358, #139037 ) ;
#50374=VECTOR ( 'NONE', #62146, 1000.000000000000114 ) ;
#50375=FACE_BOUND ( 'NONE', #5221, .T. ) ;
#50376=LINE ( 'NONE', #4656, #87297 ) ;
#50378=FACE_OUTER_BOUND ( 'NONE', #84550, .T. ) ;
#50379=CARTESIAN_POINT ( 'NONE',  ( 16.49999999999988276, -20.53675388469229190, 2.352720554255931518 ) ) ;
#50380=ORIENTED_EDGE ( 'NONE', *, *, #110189, .F. ) ;
#50381=VECTOR ( 'NONE', #28825, 1000.000000000000000 ) ;
#50382=VECTOR ( 'NONE', #85664, 999.9999999999998863 ) ;
#50383=FACE_OUTER_BOUND ( 'NONE', #104889, .T. ) ;
#50385=AXIS2_PLACEMENT_3D ( 'NONE', #38933, #26629, #83154 ) ;
#50386=VERTEX_POINT ( 'NONE', #14280 ) ;
#50388=ORIENTED_EDGE ( 'NONE', *, *, #99478, .T. ) ;
#50389=CARTESIAN_POINT ( 'NONE',  ( 34.92499999999998295, 22.22500000000000142, 4.500000000000000888 ) ) ;
#50390=EDGE_CURVE ( 'NONE', #88912, #60182, #102010, .T. ) ;
#50391=VECTOR ( 'NONE', #104151, 1000.000000000000227 ) ;
#50392=CARTESIAN_POINT ( 'NONE',  ( -25.49999999999982236, 13.46639925780212721, 5.000000000000000000 ) ) ;
#50393=DIRECTION ( 'NONE',  ( -0.7071067811865486830, 0.7071067811865464625, 0.000000000000000000 ) ) ;
#50395=EDGE_CURVE ( 'NONE', #70864, #118081, #25146, .T. ) ;
#50396=CARTESIAN_POINT ( 'NONE',  ( 32.99999999999977973, -1.447814304570818500, 5.000000000000000000 ) ) ;
#50397=ORIENTED_EDGE ( 'NONE', *, *, #73020, .F. ) ;
#50398=CARTESIAN_POINT ( 'NONE',  ( 35.99451991528749772, 28.92564299267963079, 4.000000000000000000 ) ) ;
#50399=DIRECTION ( 'NONE',  ( -0.3543493200069162685, -0.000000000000000000, -0.9351131265310288487 ) ) ;
#50400=PLANE ( 'NONE',  #112941 ) ;
#50401=DIRECTION ( 'NONE',  ( 0.7071067811865487940, 0.7071067811865463515, 0.000000000000000000 ) ) ;
#50402=FACE_OUTER_BOUND ( 'NONE', #60238, .T. ) ;
#50403=PLANE ( 'NONE',  #81727 ) ;
#50404=DIRECTION ( 'NONE',  ( 0.7071067811865486830, -0.7071067811865464625, -0.000000000000000000 ) ) ;
#50406=VERTEX_POINT ( 'NONE', #26594 ) ;
#50407=EDGE_CURVE ( 'NONE', #474, #57341, #62816, .T. ) ;
#50408=PLANE ( 'NONE',  #84324 ) ;
#50409=CARTESIAN_POINT ( 'NONE',  ( -24.48921356237309510, -27.52281430457072631, 5.000000000000000000 ) ) ;
#50411=ORIENTED_EDGE ( 'NONE', *, *, #116362, .F. ) ;
#50413=EDGE_CURVE ( 'NONE', #24882, #99874, #83865, .T. ) ;
#50416=AXIS2_PLACEMENT_3D ( 'NONE', #109217, #20049, #133146 ) ;
#50417=VERTEX_POINT ( 'NONE', #138213 ) ;
#50418=EDGE_CURVE ( 'NONE', #25547, #49111, #48344, .T. ) ;
#50421=EDGE_CURVE ( 'NONE', #26574, #30925, #117847, .T. ) ;
#50422=ORIENTED_EDGE ( 'NONE', *, *, #104100, .F. ) ;
#50423=CARTESIAN_POINT ( 'NONE',  ( 2.999999999999983569, -3.033600742197712030, 5.000000000000000000 ) ) ;
#50425=DIRECTION ( 'NONE',  ( 0.7071067811865487940, 0.7071067811865463515, 0.000000000000000000 ) ) ;
#50426=DIRECTION ( 'NONE',  ( -0.7071067811865486830, -0.7071067811865464625, 0.000000000000000000 ) ) ;
#50427=ADVANCED_FACE ( 'NONE', ( #49081 ), #104859, .F. ) ;
#50428=FACE_OUTER_BOUND ( 'NONE', #2721, .T. ) ;
#50429=EDGE_LOOP ( 'NONE', ( #59155, #73399, #3653, #112498 ) ) ;
#50430=ORIENTED_EDGE ( 'NONE', *, *, #126752, .F. ) ;
#50431=( BOUNDED_CURVE ( )  B_SPLINE_CURVE ( 3, ( #81290, #125493, #15256, #107285 ),
 .UNSPECIFIED., .F., .F. ) 
 B_SPLINE_CURVE_WITH_KNOTS ( ( 4, 4 ),
 ( 5.043186909253409844, 5.074607125596340751 ),
 .UNSPECIFIED. ) 
 CURVE ( )  GEOMETRIC_REPRESENTATION_ITEM ( )  RATIONAL_B_SPLINE_CURVE ( ( 1.000000000000000000, 0.9999177325257868620, 0.9999177325257868620, 1.000000000000000000 ) ) 
 REPRESENTATION_ITEM ( '' )  );
#50432=FACE_OUTER_BOUND ( 'NONE', #137374, .T. ) ;
#50434=VERTEX_POINT ( 'NONE', #72290 ) ;
#50436=VERTEX_POINT ( 'NONE', #5524 ) ;
#50438=ORIENTED_EDGE ( 'NONE', *, *, #6260, .T. ) ;
#50439=ORIENTED_EDGE ( 'NONE', *, *, #94890, .F. ) ;
#50441=CARTESIAN_POINT ( 'NONE',  ( -31.82816939922330945, 0.7592924766157069794, 4.000000000000000000 ) ) ;
#50443=CARTESIAN_POINT ( 'NONE',  ( 11.99999999999992006, 12.83542986846998168, -1.025386466790397577 ) ) ;
#50444=DIRECTION ( 'NONE',  ( -0.000000000000000000, -0.3543493200069152693, 0.9351131265310292928 ) ) ;
#50445=CARTESIAN_POINT ( 'NONE',  ( 17.99999999999987566, -15.03360074219758502, 5.000000000000000000 ) ) ;
#50446=VERTEX_POINT ( 'NONE', #18533 ) ;
#50447=PLANE ( 'NONE',  #134679 ) ;
#50448=ORIENTED_EDGE ( 'NONE', *, *, #91955, .T. ) ;
#50450=EDGE_CURVE ( 'NONE', #120651, #102811, #70835, .T. ) ;
#50452=DIRECTION ( 'NONE',  ( -0.000000000000000000, -0.000000000000000000, 1.000000000000000000 ) ) ;
#50454=VECTOR ( 'NONE', #58819, 1000.000000000000000 ) ;
#50455=DIRECTION ( 'NONE',  ( -0.6830127018922180770, -0.6830127018922204085, -0.2588190451025213501 ) ) ;
#50456=ORIENTED_EDGE ( 'NONE', *, *, #99925, .F. ) ;
#50457=ORIENTED_EDGE ( 'NONE', *, *, #15855, .T. ) ;
#50458=ORIENTED_EDGE ( 'NONE', *, *, #51678, .T. ) ;
#50459=DIRECTION ( 'NONE',  ( 0.7071067811865486830, -0.7071067811865464625, -0.000000000000000000 ) ) ;
#50460=DIRECTION ( 'NONE',  ( -0.7071067811865487940, 0.7071067811865463515, -0.000000000000000000 ) ) ;
#50461=LINE ( 'NONE', #60660, #45411 ) ;
#50462=CARTESIAN_POINT ( 'NONE',  ( 2.602085213965210642E-15, -15.03360074219759035, 5.000000000000000000 ) ) ;
#50463=EDGE_CURVE ( 'NONE', #125435, #50934, #4060, .T. ) ;
#50466=CARTESIAN_POINT ( 'NONE',  ( -30.29974487139158867, -27.71228299555227537, 4.000000000000000000 ) ) ;
#50467=CARTESIAN_POINT ( 'NONE',  ( 32.29289321881323360, 20.25929247661551713, 5.000000000000000000 ) ) ;
#50468=VECTOR ( 'NONE', #24111, 1000.000000000000000 ) ;
#50469=DIRECTION ( 'NONE',  ( 0.7071067811865486830, -0.7071067811865464625, -0.000000000000000000 ) ) ;
#50471=CARTESIAN_POINT ( 'NONE',  ( -2.510786437626908008, -27.52281430457053446, 5.000000000000000000 ) ) ;
#50472=ORIENTED_EDGE ( 'NONE', *, *, #90940, .T. ) ;
#50473=CARTESIAN_POINT ( 'NONE',  ( 28.49999999999979750, 3.431123077392151277, 4.000000000000000000 ) ) ;
#50474=ORIENTED_EDGE ( 'NONE', *, *, #41705, .F. ) ;
#50475=LINE ( 'NONE', #94661, #66959 ) ;
#50476=PLANE ( 'NONE',  #39509 ) ;
#50477=VERTEX_POINT ( 'NONE', #93270 ) ;
#50478=VECTOR ( 'NONE', #37179, 1000.000000000000000 ) ;
#50479=LINE ( 'NONE', #92521, #120439 ) ;
#50480=LINE ( 'NONE', #126580, #65758 ) ;
#50482=ORIENTED_EDGE ( 'NONE', *, *, #122197, .T. ) ;
#50484=DIRECTION ( 'NONE',  ( 1.000000000000000000, 0.000000000000000000, 0.000000000000000000 ) ) ;
#50485=AXIS2_PLACEMENT_3D ( 'NONE', #70232, #116537, #93358 ) ;
#50486=VECTOR ( 'NONE', #83380, 1000.000000000000227 ) ;
#50487=LINE ( 'NONE', #17819, #93919 ) ;
#50489=PLANE ( 'NONE',  #44060 ) ;
#50490=ORIENTED_EDGE ( 'NONE', *, *, #92239, .F. ) ;
#50491=LINE ( 'NONE', #141800, #51557 ) ;
#50492=EDGE_CURVE ( 'NONE', #6418, #81300, #17147, .T. ) ;
#50493=DIRECTION ( 'NONE',  ( -0.7071067811865487940, 0.7071067811865463515, 0.000000000000000000 ) ) ;
#50496=LINE ( 'NONE', #117151, #95389 ) ;
#50497=ORIENTED_EDGE ( 'NONE', *, *, #122873, .F. ) ;
#50498=FACE_OUTER_BOUND ( 'NONE', #42131, .T. ) ;
#50499=EDGE_CURVE ( 'NONE', #105033, #24914, #49805, .T. ) ;
#50502=CARTESIAN_POINT ( 'NONE',  ( -45.18398860626900415, 28.73617430169818832, 5.000000000000000000 ) ) ;
#50503=FACE_OUTER_BOUND ( 'NONE', #44058, .T. ) ;
#50504=LINE ( 'NONE', #93988, #29349 ) ;
#50505=ORIENTED_EDGE ( 'NONE', *, *, #23009, .T. ) ;
#50507=EDGE_CURVE ( 'NONE', #50434, #18880, #62098, .T. ) ;
#50508=CARTESIAN_POINT ( 'NONE',  ( -30.79289321881323716, 18.75929247661552068, 5.000000000000000000 ) ) ;
#50510=EDGE_CURVE ( 'NONE', #23479, #15065, #15664, .T. ) ;
#50511=CARTESIAN_POINT ( 'NONE',  ( 9.005480084712511157, 28.92564299267931816, 4.000000000000000000 ) ) ;
#50512=ORIENTED_EDGE ( 'NONE', *, *, #2387, .F. ) ;
#50513=CARTESIAN_POINT ( 'NONE',  ( 20.51078643762690490, -27.52281430457041012, 5.000000000000000000 ) ) ;
#50517=EDGE_CURVE ( 'NONE', #126622, #115239, #104114, .T. ) ;
#50518=ADVANCED_FACE ( 'NONE', ( #61412 ), #4778, .F. ) ;
#50519=ORIENTED_EDGE ( 'NONE', *, *, #80792, .T. ) ;
#50520=ORIENTED_EDGE ( 'NONE', *, *, #61151, .F. ) ;
#50523=ADVANCED_FACE ( 'NONE', ( #127320 ), #6218, .F. ) ;
#50524=CARTESIAN_POINT ( 'NONE',  ( -2.510786437626908008, -27.52281430457053446, 5.000000000000000000 ) ) ;
#50525=LINE ( 'NONE', #28786, #31543 ) ;
#50526=ORIENTED_EDGE ( 'NONE', *, *, #126688, .T. ) ;
#50527=AXIS2_PLACEMENT_3D ( 'NONE', #78231, #76078, #88397 ) ;
#50528=DIRECTION ( 'NONE',  ( -0.000000000000000000, 0.3543493200069153248, 0.9351131265310292928 ) ) ;
#50529=DIRECTION ( 'NONE',  ( -0.7071067811865487940, 0.7071067811865463515, -0.000000000000000000 ) ) ;
#50530=AXIS2_PLACEMENT_3D ( 'NONE', #114792, #3195, #47482 ) ;
#50531=EDGE_CURVE ( 'NONE', #141627, #136986, #120726, .T. ) ;
#50532=EDGE_LOOP ( 'NONE', ( #30223, #122447, #121831, #64838 ) ) ;
#50533=CARTESIAN_POINT ( 'NONE',  ( -24.87009481391958943, 1.845822036158551560, 4.338987337627235874 ) ) ;
#50534=DIRECTION ( 'NONE',  ( 0.7071067811865487940, 0.7071067811865463515, 0.000000000000000000 ) ) ;
#50535=EDGE_CURVE ( 'NONE', #34536, #6676, #77273, .T. ) ;
#50536=ORIENTED_EDGE ( 'NONE', *, *, #129057, .F. ) ;
#50537=EDGE_LOOP ( 'NONE', ( #16250, #45067, #130729, #59383 ) ) ;
#50538=LINE ( 'NONE', #15712, #91734 ) ;
#50539=FACE_OUTER_BOUND ( 'NONE', #20997, .T. ) ;
#50540=CARTESIAN_POINT ( 'NONE',  ( 3.489213562373097322, -27.52281430457057709, 5.000000000000000000 ) ) ;
#50541=CARTESIAN_POINT ( 'NONE',  ( -2.588385094051669721, 22.22500000000000142, 4.777194822843815025 ) ) ;
#50542=EDGE_CURVE ( 'NONE', #41817, #20431, #143205, .T. ) ;
#50543=CARTESIAN_POINT ( 'NONE',  ( 0.000000000000000000, -21.72500000000000142, 4.500000000000000888 ) ) ;
#50544=FACE_OUTER_BOUND ( 'NONE', #69076, .T. ) ;
#50547=EDGE_LOOP ( 'NONE', ( #137037, #11581, #25456, #37510 ) ) ;
#50549=ADVANCED_FACE ( 'NONE', ( #131629 ), #132369, .F. ) ;
#50551=ADVANCED_FACE ( 'NONE', ( #21434 ), #108387, .F. ) ;
#50552=EDGE_CURVE ( 'NONE', #124775, #39127, #33063, .T. ) ;
#50554=ORIENTED_EDGE ( 'NONE', *, *, #59259, .T. ) ;
#50556=CARTESIAN_POINT ( 'NONE',  ( -27.29974487139158512, -27.71228299555225405, 4.000000000000000000 ) ) ;
#50557=CARTESIAN_POINT ( 'NONE',  ( -6.693269933095949753, -3.740707523384248390, 12.88036043432869171 ) ) ;
#50558=DIRECTION ( 'NONE',  ( 0.7071067811865487940, 0.7071067811865463515, 0.000000000000000000 ) ) ;
#50559=VECTOR ( 'NONE', #12911, 1000.000000000000000 ) ;
#50561=CARTESIAN_POINT ( 'NONE',  ( -15.07337884938728045, -22.22500000000000142, 12.52252134653477533 ) ) ;
#50562=VERTEX_POINT ( 'NONE', #98967 ) ;
#50563=EDGE_CURVE ( 'NONE', #139694, #113402, #64951, .T. ) ;
#50564=FACE_OUTER_BOUND ( 'NONE', #112501, .T. ) ;
#50566=VECTOR ( 'NONE', #49686, 1000.000000000000000 ) ;
#50567=VERTEX_POINT ( 'NONE', #85239 ) ;
#50568=FACE_OUTER_BOUND ( 'NONE', #44011, .T. ) ;
#50569=EDGE_LOOP ( 'NONE', ( #114392, #136998, #66920, #1995 ) ) ;
#50571=VECTOR ( 'NONE', #11353, 1000.000000000000000 ) ;
#50574=ORIENTED_EDGE ( 'NONE', *, *, #85471, .T. ) ;
#50576=VECTOR ( 'NONE', #102310, 999.9999999999998863 ) ;
#50577=VERTEX_POINT ( 'NONE', #52617 ) ;
#50578=VECTOR ( 'NONE', #94936, 1000.000000000000000 ) ;
#50579=DIRECTION ( 'NONE',  ( -0.3543493200069162685, -0.000000000000000000, -0.9351131265310288487 ) ) ;
#50580=DIRECTION ( 'NONE',  ( 0.7071067811865487940, -0.7071067811865463515, 0.000000000000000000 ) ) ;
#50582=( BOUNDED_CURVE ( )  B_SPLINE_CURVE ( 3, ( #81823, #57213, #136160, #103510 ),
 .UNSPECIFIED., .F., .T. ) 
 B_SPLINE_CURVE_WITH_KNOTS ( ( 4, 4 ),
 ( 3.858351980207633591, 3.926990816987243615 ),
 .UNSPECIFIED. ) 
 CURVE ( )  GEOMETRIC_REPRESENTATION_ITEM ( )  RATIONAL_B_SPLINE_CURVE ( ( 1.000000000000000000, 0.9996074310407765395, 0.9996074310407765395, 1.000000000000000000 ) ) 
 REPRESENTATION_ITEM ( '' )  );
#50583=FACE_OUTER_BOUND ( 'NONE', #132176, .T. ) ;
#50584=EDGE_CURVE ( 'NONE', #12119, #9403, #54789, .T. ) ;
#50585=DIRECTION ( 'NONE',  ( -0.7071067811865486830, -0.7071067811865464625, 0.000000000000000000 ) ) ;
#50586=DIRECTION ( 'NONE',  ( -0.000000000000000000, -0.3543493200069152693, 0.9351131265310292928 ) ) ;
#50588=ADVANCED_FACE ( 'NONE', ( #43198 ), #141801, .F. ) ;
#50589=CARTESIAN_POINT ( 'NONE',  ( 57.48921356237308800, -27.52281430457095368, 5.000000000000000000 ) ) ;
#50590=DIRECTION ( 'NONE',  ( -0.7071067811865486830, -0.7071067811865464625, 0.000000000000000000 ) ) ;
#50591=DIRECTION ( 'NONE',  ( -0.7071067811865487940, 0.7071067811865463515, 0.000000000000000000 ) ) ;
#50592=ORIENTED_EDGE ( 'NONE', *, *, #20617, .F. ) ;
#50593=AXIS2_PLACEMENT_3D ( 'NONE', #105017, #51374, #115149 ) ;
#50595=CARTESIAN_POINT ( 'NONE',  ( -18.08491323193750588, -12.74070752338414181, 18.74364270924349896 ) ) ;
#50596=VERTEX_POINT ( 'NONE', #10528 ) ;
#50597=ORIENTED_EDGE ( 'NONE', *, *, #124828, .T. ) ;
#50598=CARTESIAN_POINT ( 'NONE',  ( -60.18398860626900415, 28.73617430169829490, 5.000000000000000000 ) ) ;
#50599=ORIENTED_EDGE ( 'NONE', *, *, #93110, .T. ) ;
#50600=AXIS2_PLACEMENT_3D ( 'NONE', #47653, #71517, #91815 ) ;
#50601=DIRECTION ( 'NONE',  ( 0.7071067811865487940, 0.7071067811865463515, 0.000000000000000000 ) ) ;
#50604=DIRECTION ( 'NONE',  ( -0.3543493200069162685, -0.000000000000000000, -0.9351131265310288487 ) ) ;
#50606=ORIENTED_EDGE ( 'NONE', *, *, #65513, .F. ) ;
#50608=EDGE_LOOP ( 'NONE', ( #94120, #104801, #27167, #101356 ) ) ;
#50612=DIRECTION ( 'NONE',  ( 0.7071067811865487940, 0.7071067811865463515, 0.000000000000000000 ) ) ;
#50613=CARTESIAN_POINT ( 'NONE',  ( 14.29289321881336328, -6.740707523384209310, 5.000000000000000000 ) ) ;
#50614=CARTESIAN_POINT ( 'NONE',  ( -21.83829387547366707, -6.740707523384205757, 16.75550250614861980 ) ) ;
#50615=ORIENTED_EDGE ( 'NONE', *, *, #115615, .T. ) ;
#50616=ORIENTED_EDGE ( 'NONE', *, *, #2197, .T. ) ;
#50617=ORIENTED_EDGE ( 'NONE', *, *, #111430, .T. ) ;
#50618=CARTESIAN_POINT ( 'NONE',  ( 32.67183060077623935, -3.740707523384248390, 4.000000000000000000 ) ) ;
#50619=PLANE ( 'NONE',  #129824 ) ;
#50620=LINE ( 'NONE', #94105, #40471 ) ;
#50621=AXIS2_PLACEMENT_3D ( 'NONE', #109079, #9774, #54041 ) ;
#50623=DIRECTION ( 'NONE',  ( 0.6830127018922180770, -0.6830127018922204085, -0.2588190451025213501 ) ) ;
#50624=VECTOR ( 'NONE', #108910, 1000.000000000000227 ) ;
#50626=CARTESIAN_POINT ( 'NONE',  ( -5.999999999999956479, -7.068876922607738145, 4.000000000000000000 ) ) ;
#50627=DIRECTION ( 'NONE',  ( -0.000000000000000000, 0.000000000000000000, 1.000000000000000000 ) ) ;
#50629=EDGE_LOOP ( 'NONE', ( #77293, #78, #79280, #70921 ) ) ;
#50630=CARTESIAN_POINT ( 'NONE',  ( 36.18398860626899705, 28.73617430169812437, 5.000000000000000000 ) ) ;
#50631=CARTESIAN_POINT ( 'NONE',  ( -3.005480084712505828, 28.92564299267936079, 4.000000000000000000 ) ) ;
#50632=EDGE_LOOP ( 'NONE', ( #114362, #119325, #96165, #128514 ) ) ;
#50633=CARTESIAN_POINT ( 'NONE',  ( -26.29289321881326558, 17.25929247661554200, 5.000000000000000000 ) ) ;
#50634=DIRECTION ( 'NONE',  ( 0.6830127018922181881, 0.6830127018922202975, -0.2588190451025214056 ) ) ;
#50635=VERTEX_POINT ( 'NONE', #53328 ) ;
#50636=LINE ( 'NONE', #62244, #118622 ) ;
#50637=CARTESIAN_POINT ( 'NONE',  ( -60.18398860626900415, 28.73617430169829490, 5.000000000000000000 ) ) ;
#50639=LINE ( 'NONE', #17970, #30489 ) ;
#50641=ORIENTED_EDGE ( 'NONE', *, *, #138909, .F. ) ;
#50642=CARTESIAN_POINT ( 'NONE',  ( 34.92499999999998295, 22.22500000000000142, 4.000000000000000000 ) ) ;
#50643=( BOUNDED_CURVE ( )  B_SPLINE_CURVE ( 3, ( #81434, #50211, #39343, #61811 ),
 .UNSPECIFIED., .F., .T. ) 
 B_SPLINE_CURVE_WITH_KNOTS ( ( 4, 4 ),
 ( 1.864375635226928729, 1.933014472006545859 ),
 .UNSPECIFIED. ) 
 CURVE ( )  GEOMETRIC_REPRESENTATION_ITEM ( )  RATIONAL_B_SPLINE_CURVE ( ( 1.000000000000000000, 0.9996074310407763175, 0.9996074310407763175, 1.000000000000000000 ) ) 
 REPRESENTATION_ITEM ( '' )  );
#50645=CARTESIAN_POINT ( 'NONE',  ( -21.18398860626899349, 28.73617430169802134, 5.000000000000000000 ) ) ;
#50646=LINE ( 'NONE', #106408, #101499 ) ;
#50647=CARTESIAN_POINT ( 'NONE',  ( 1.171830600776462061, -17.24070752338410628, 4.000000000000000000 ) ) ;
#50648=CARTESIAN_POINT ( 'NONE',  ( 27.29974487139158512, -27.71228299555225405, 4.000000000000000000 ) ) ;
#50649=CARTESIAN_POINT ( 'NONE',  ( -17.81601139373099940, 28.73617430169775133, 5.000000000000000000 ) ) ;
#50653=PLANE ( 'NONE',  #88376 ) ;
#50654=DIRECTION ( 'NONE',  ( 0.7071067811865487940, 0.7071067811865463515, -0.000000000000000000 ) ) ;
#50655=ORIENTED_EDGE ( 'NONE', *, *, #36969, .T. ) ;
#50656=ORIENTED_EDGE ( 'NONE', *, *, #3947, .F. ) ;
#50658=ORIENTED_EDGE ( 'NONE', *, *, #66978, .F. ) ;
#50660=CARTESIAN_POINT ( 'NONE',  ( -8.700255128608413102, -27.71228299555199825, 4.000000000000000000 ) ) ;
#50661=FACE_OUTER_BOUND ( 'NONE', #143161, .T. ) ;
#50662=ORIENTED_EDGE ( 'NONE', *, *, #34573, .T. ) ;
#50664=VECTOR ( 'NONE', #43153, 1000.000000000000000 ) ;
#50666=LINE ( 'NONE', #126783, #122716 ) ;
#50667=DIRECTION ( 'NONE',  ( 0.6830127018922180770, -0.6830127018922204085, -0.2588190451025213501 ) ) ;
#50668=VECTOR ( 'NONE', #139905, 1000.000000000000000 ) ;
#50669=EDGE_CURVE ( 'NONE', #130020, #52896, #92963, .T. ) ;
#50670=CARTESIAN_POINT ( 'NONE',  ( -11.99999999999991473, -3.412538124160724884, 4.000000000000000000 ) ) ;
#50671=CARTESIAN_POINT ( 'NONE',  ( 17.99999999999988276, -13.39766691384881092, -10.96608748226469565 ) ) ;
#50673=ADVANCED_FACE ( 'NONE', ( #96114 ), #140348, .T. ) ;
#50675=CARTESIAN_POINT ( 'NONE',  ( -24.34427593291135139, 5.931737808750704666, 4.000000000000000000 ) ) ;
#50678=CARTESIAN_POINT ( 'NONE',  ( -11.51078643762690490, -27.52281430457047406, 5.000000000000000000 ) ) ;
#50679=CARTESIAN_POINT ( 'NONE',  ( 33.48921356237309510, -27.52281430457078670, 5.000000000000000000 ) ) ;
#50680=DIRECTION ( 'NONE',  ( -0.3543493200069162685, -0.000000000000000000, -0.9351131265310288487 ) ) ;
#50681=VECTOR ( 'NONE', #132861, 1000.000000000000000 ) ;
#50682=CARTESIAN_POINT ( 'NONE',  ( -9.183988606268997046, 28.73617430169793607, 5.000000000000000000 ) ) ;
#50684=EDGE_CURVE ( 'NONE', #106952, #65100, #142512, .T. ) ;
#50685=EDGE_CURVE ( 'NONE', #93631, #39593, #41755, .T. ) ;
#50686=EDGE_LOOP ( 'NONE', ( #100527, #138902, #140958, #124658 ) ) ;
#50687=ORIENTED_EDGE ( 'NONE', *, *, #7824, .T. ) ;
#50689=EDGE_LOOP ( 'NONE', ( #103570, #139139, #52619, #118410 ) ) ;
#50690=ADVANCED_FACE ( 'NONE', ( #122879 ), #11961, .F. ) ;
#50693=EDGE_CURVE ( 'NONE', #57164, #66617, #68531, .T. ) ;
#50694=PLANE ( 'NONE',  #110251 ) ;
#50695=ORIENTED_EDGE ( 'NONE', *, *, #61450, .F. ) ;
#50696=CARTESIAN_POINT ( 'NONE',  ( 0.000000000000000000, 0.000000000000000000, 5.000000000000000000 ) ) ;
#50697=DIRECTION ( 'NONE',  ( 0.6830127018922181881, 0.6830127018922202975, -0.2588190451025214056 ) ) ;
#50698=EDGE_CURVE ( 'NONE', #130424, #76656, #90243, .T. ) ;
#50699=AXIS2_PLACEMENT_3D ( 'NONE', #47510, #57648, #89530 ) ;
#50701=VERTEX_POINT ( 'NONE', #58394 ) ;
#50702=CARTESIAN_POINT ( 'NONE',  ( -34.42500000000001137, 0.000000000000000000, 4.500000000000000888 ) ) ;
#50703=ORIENTED_EDGE ( 'NONE', *, *, #60189, .T. ) ;
#50704=LINE ( 'NONE', #128275, #80083 ) ;
#50705=CARTESIAN_POINT ( 'NONE',  ( -59.99451991528749772, 28.92564299267980132, 4.000000000000000000 ) ) ;
#50706=DIRECTION ( 'NONE',  ( -0.000000000000000000, 0.000000000000000000, 1.000000000000000000 ) ) ;
#50707=AXIS2_PLACEMENT_3D ( 'NONE', #69995, #125036, #24995 ) ;
#50708=DIRECTION ( 'NONE',  ( 0.6830127018922180770, -0.6830127018922204085, -0.2588190451025213501 ) ) ;
#50710=EDGE_CURVE ( 'NONE', #3311, #63026, #11222, .T. ) ;
#50711=VECTOR ( 'NONE', #33881, 999.9999999999998863 ) ;
#50712=ORIENTED_EDGE ( 'NONE', *, *, #5662, .T. ) ;
#50713=ORIENTED_EDGE ( 'NONE', *, *, #49723, .T. ) ;
#50714=EDGE_LOOP ( 'NONE', ( #138632, #14018, #119132, #84289 ) ) ;
#50715=LINE ( 'NONE', #126138, #132542 ) ;
#50718=EDGE_CURVE ( 'NONE', #105033, #58332, #55501, .T. ) ;
#50720=EDGE_LOOP ( 'NONE', ( #41844, #66879, #18225, #106360 ) ) ;
#50722=CARTESIAN_POINT ( 'NONE',  ( -13.22578070446010301, 4.485909045323550615, 4.327832195654622183 ) ) ;
#50724=ORIENTED_EDGE ( 'NONE', *, *, #27860, .F. ) ;
#50725=EDGE_CURVE ( 'NONE', #55173, #43690, #133765, .T. ) ;
#50728=ADVANCED_FACE ( 'NONE', ( #33760 ), #56945, .F. ) ;
#50729=DIRECTION ( 'NONE',  ( 0.7071067811865487940, 0.7071067811865463515, -0.000000000000000000 ) ) ;
#50730=DIRECTION ( 'NONE',  ( -0.000000000000000000, 0.3543493200069153248, 0.9351131265310292928 ) ) ;
#50731=ORIENTED_EDGE ( 'NONE', *, *, #119286, .T. ) ;
#50732=CARTESIAN_POINT ( 'NONE',  ( -21.18398860626899349, 28.73617430169802134, 5.000000000000000000 ) ) ;
#50733=EDGE_CURVE ( 'NONE', #68374, #101800, #44656, .T. ) ;
#50734=CARTESIAN_POINT ( 'NONE',  ( 30.18398860626900060, 28.73617430169808173, 5.000000000000000000 ) ) ;
#50735=CARTESIAN_POINT ( 'NONE',  ( -34.42500000000001137, 0.000000000000000000, 4.500000000000000888 ) ) ;
#50737=VERTEX_POINT ( 'NONE', #102577 ) ;
#50738=ADVANCED_FACE ( 'NONE', ( #101116 ), #13376, .F. ) ;
#50739=CARTESIAN_POINT ( 'NONE',  ( 68.99451991528748351, 28.92564299267986172, 4.000000000000000000 ) ) ;
#50740=FACE_BOUND ( 'NONE', #92790, .T. ) ;
#50741=ORIENTED_EDGE ( 'NONE', *, *, #80202, .F. ) ;
#50742=FACE_OUTER_BOUND ( 'NONE', #93197, .T. ) ;
#50743=CARTESIAN_POINT ( 'NONE',  ( 3.423278458063512719, 11.25929247661559529, 17.85071094206583808 ) ) ;
#50746=CARTESIAN_POINT ( 'NONE',  ( 27.48921356237309155, -27.52281430457074762, 5.000000000000000000 ) ) ;
#50747=ORIENTED_EDGE ( 'NONE', *, *, #47048, .F. ) ;
#50748=ORIENTED_EDGE ( 'NONE', *, *, #21836, .T. ) ;
#50749=EDGE_CURVE ( 'NONE', #134120, #101708, #99686, .T. ) ;
#50750=ORIENTED_EDGE ( 'NONE', *, *, #88891, .T. ) ;
#50753=DIRECTION ( 'NONE',  ( -0.000000000000000000, 0.3543493200069153248, 0.9351131265310292928 ) ) ;
#50754=LINE ( 'NONE', #96356, #80892 ) ;
#50755=LINE ( 'NONE', #6475, #56689 ) ;
#50756=EDGE_CURVE ( 'NONE', #9912, #91707, #135898, .T. ) ;
#50757=DIRECTION ( 'NONE',  ( -0.000000000000000000, 0.3543493200069153248, 0.9351131265310292928 ) ) ;
#50758=FACE_OUTER_BOUND ( 'NONE', #33383, .T. ) ;
#50759=CARTESIAN_POINT ( 'NONE',  ( 54.48921356237310221, -27.52281430457093236, 5.000000000000000000 ) ) ;
#50760=LINE ( 'NONE', #20246, #29785 ) ;
#50761=DIRECTION ( 'NONE',  ( -0.7071067811865487940, 0.7071067811865463515, 0.000000000000000000 ) ) ;
#50762=CARTESIAN_POINT ( 'NONE',  ( -20.16347128873438521, 15.75929247661555799, 9.299976744542872709 ) ) ;
#50763=VERTEX_POINT ( 'NONE', #36575 ) ;
#50764=ORIENTED_EDGE ( 'NONE', *, *, #605, .F. ) ;
#50765=VECTOR ( 'NONE', #8750, 1000.000000000000114 ) ;
#50766=VERTEX_POINT ( 'NONE', #123630 ) ;
#50767=VERTEX_POINT ( 'NONE', #80824 ) ;
#50769=VECTOR ( 'NONE', #5270, 1000.000000000000114 ) ;
#50770=VECTOR ( 'NONE', #59061, 1000.000000000000000 ) ;
#50771=ORIENTED_EDGE ( 'NONE', *, *, #105014, .F. ) ;
#50775=DIRECTION ( 'NONE',  ( 0.7071067811865486830, -0.7071067811865464625, -0.000000000000000000 ) ) ;
#50776=ADVANCED_FACE ( 'NONE', ( #125015 ), #57653, .F. ) ;
#50777=DIRECTION ( 'NONE',  ( -0.000000000000000000, -0.3543493200069152693, 0.9351131265310292928 ) ) ;
#50778=ORIENTED_EDGE ( 'NONE', *, *, #57502, .F. ) ;
#50781=EDGE_LOOP ( 'NONE', ( #80223, #81641, #113387, #2794 ) ) ;
#50782=CARTESIAN_POINT ( 'NONE',  ( 34.49999999999976552, 21.05432934483073026, 4.994342998332161443 ) ) ;
#50785=ORIENTED_EDGE ( 'NONE', *, *, #108991, .F. ) ;
#50787=LINE ( 'NONE', #106556, #113788 ) ;
#50788=LINE ( 'NONE', #117438, #55847 ) ;
#50789=VERTEX_POINT ( 'NONE', #66376 ) ;
#50790=ORIENTED_EDGE ( 'NONE', *, *, #98081, .T. ) ;
#50791=DIRECTION ( 'NONE',  ( -0.6830127018922180770, -0.6830127018922204085, -0.2588190451025213501 ) ) ;
#50795=AXIS2_PLACEMENT_3D ( 'NONE', #122092, #133018, #141742 ) ;
#50796=CARTESIAN_POINT ( 'NONE',  ( -30.18398860626900060, 28.73617430169808173, 5.000000000000000000 ) ) ;
#50797=CARTESIAN_POINT ( 'NONE',  ( -21.79289321881330110, 18.75929247661552779, 5.000000000000000000 ) ) ;
#50798=LINE ( 'NONE', #63128, #5647 ) ;
#50800=EDGE_LOOP ( 'NONE', ( #104731, #24592, #76958 ) ) ;
#50801=EDGE_CURVE ( 'NONE', #141779, #140054, #78670, .T. ) ;
#50803=AXIS2_PLACEMENT_3D ( 'NONE', #77787, #902, #35744 ) ;
#50804=EDGE_CURVE ( 'NONE', #14634, #131639, #124306, .T. ) ;
#50805=LINE ( 'NONE', #53672, #218 ) ;
#50806=DIRECTION ( 'NONE',  ( -0.7071067811865486830, -0.7071067811865464625, 0.000000000000000000 ) ) ;
#50810=CARTESIAN_POINT ( 'NONE',  ( 8.994519915287490619, 28.92564299267944250, 4.000000000000000000 ) ) ;
#50812=ORIENTED_EDGE ( 'NONE', *, *, #11047, .T. ) ;
#50813=VECTOR ( 'NONE', #121413, 1000.000000000000000 ) ;
#50815=ORIENTED_EDGE ( 'NONE', *, *, #3240, .F. ) ;
#50816=EDGE_CURVE ( 'NONE', #15918, #76576, #109476, .T. ) ;
#50817=VECTOR ( 'NONE', #76201, 1000.000000000000000 ) ;
#50818=ORIENTED_EDGE ( 'NONE', *, *, #136700, .T. ) ;
#50820=VECTOR ( 'NONE', #65859, 1000.000000000000000 ) ;
#50823=FACE_OUTER_BOUND ( 'NONE', #21142, .T. ) ;
#50824=VECTOR ( 'NONE', #101220, 1000.000000000000000 ) ;
#50825=DIRECTION ( 'NONE',  ( -0.6830127018922181881, 0.6830127018922202975, -0.2588190451025214056 ) ) ;
#50826=DIRECTION ( 'NONE',  ( -0.7071067811865487940, 0.7071067811865463515, 0.000000000000000000 ) ) ;
#50828=CARTESIAN_POINT ( 'NONE',  ( -34.92500000000001137, -22.22500000000000142, 4.000000000000000000 ) ) ;
#50829=CARTESIAN_POINT ( 'NONE',  ( 20.74722711705611644, 22.22500000000000142, -16.09628799178753766 ) ) ;
#50830=CARTESIAN_POINT ( 'NONE',  ( 3.183988606268992161, 28.73617430169789699, 5.000000000000000000 ) ) ;
#50832=DIRECTION ( 'NONE',  ( -0.000000000000000000, 0.000000000000000000, 1.000000000000000000 ) ) ;
#50833=CARTESIAN_POINT ( 'NONE',  ( 14.51078643762690490, -27.52281430457045275, 5.000000000000000000 ) ) ;
#50835=ORIENTED_EDGE ( 'NONE', *, *, #54641, .F. ) ;
#50837=ORIENTED_EDGE ( 'NONE', *, *, #91676, .F. ) ;
#50841=ORIENTED_EDGE ( 'NONE', *, *, #4471, .F. ) ;
#50843=LINE ( 'NONE', #95033, #118007 ) ;
#50844=EDGE_LOOP ( 'NONE', ( #117220, #118608, #5736, #118339 ) ) ;
#50845=DIRECTION ( 'NONE',  ( 1.000000000000000000, 0.000000000000000000, 0.000000000000000000 ) ) ;
#50846=DIRECTION ( 'NONE',  ( -0.7071067811865487940, 0.7071067811865463515, -0.000000000000000000 ) ) ;
#50847=CARTESIAN_POINT ( 'NONE',  ( -24.18398860626899705, 28.73617430169804265, 5.000000000000000000 ) ) ;
#50848=FACE_OUTER_BOUND ( 'NONE', #15889, .T. ) ;
#50850=ORIENTED_EDGE ( 'NONE', *, *, #30784, .T. ) ;
#50851=EDGE_CURVE ( 'NONE', #62405, #137509, #22811, .T. ) ;
#50852=CARTESIAN_POINT ( 'NONE',  ( -13.27644930412397350, 4.689949953678146599, 5.000000000000000000 ) ) ;
#50853=DIRECTION ( 'NONE',  ( -0.7071067811865486830, -0.7071067811865464625, 0.000000000000000000 ) ) ;
#50854=LINE ( 'NONE', #40699, #19607 ) ;
#50855=LINE ( 'NONE', #5881, #68402 ) ;
#50856=CARTESIAN_POINT ( 'NONE',  ( -23.57672154193631542, 11.25929247661559529, 17.85071094206589493 ) ) ;
#50860=ADVANCED_FACE ( 'NONE', ( #72110 ), #84399, .F. ) ;
#50861=EDGE_CURVE ( 'NONE', #111356, #38643, #114824, .T. ) ;
#50863=VERTEX_POINT ( 'NONE', #27846 ) ;
#50866=ADVANCED_FACE ( 'NONE', ( #71367 ), #138767, .F. ) ;
#50867=ORIENTED_EDGE ( 'NONE', *, *, #114029, .T. ) ;
#50868=DIRECTION ( 'NONE',  ( -0.7071067811865486830, -0.7071067811865464625, -0.000000000000000000 ) ) ;
#50869=EDGE_CURVE ( 'NONE', #22009, #19810, #16979, .T. ) ;
#50870=CARTESIAN_POINT ( 'NONE',  ( 77.99451991528749772, 28.92564299267992567, 4.000000000000000000 ) ) ;
#50871=EDGE_CURVE ( 'NONE', #94372, #98076, #59098, .T. ) ;
#50872=CARTESIAN_POINT ( 'NONE',  ( 21.29974487139158512, -27.71228299555221142, 4.000000000000000000 ) ) ;
#50874=DIRECTION ( 'NONE',  ( -0.7071067811865487940, 0.7071067811865463515, 0.000000000000000000 ) ) ;
#50875=ADVANCED_FACE ( 'NONE', ( #27125 ), #103948, .F. ) ;
#50878=CARTESIAN_POINT ( 'NONE',  ( 2.999999999999978240, -18.03360074219755660, 5.000000000000000000 ) ) ;
#50879=EDGE_LOOP ( 'NONE', ( #19859, #8216, #52094, #8276 ) ) ;
#50880=CARTESIAN_POINT ( 'NONE',  ( -72.48921356237309510, -27.52281430457106026, 5.000000000000000000 ) ) ;
#50881=VECTOR ( 'NONE', #17780, 999.9999999999998863 ) ;
#50882=AXIS2_PLACEMENT_3D ( 'NONE', #129217, #142959, #108871 ) ;
#50883=LINE ( 'NONE', #116121, #43057 ) ;
#50884=PLANE ( 'NONE',  #122786 ) ;
#50886=AXIS2_PLACEMENT_3D ( 'NONE', #132983, #120616, #10436 ) ;
#50887=ADVANCED_FACE ( 'NONE', ( #39462 ), #126433, .F. ) ;
#50888=CARTESIAN_POINT ( 'NONE',  ( 2.994519915287485734, 28.92564299267940342, 4.000000000000000000 ) ) ;
#50889=ORIENTED_EDGE ( 'NONE', *, *, #30909, .F. ) ;
#50891=ADVANCED_FACE ( 'NONE', ( #125754 ), #3904, .T. ) ;
#50892=VERTEX_POINT ( 'NONE', #116989 ) ;
#50893=CARTESIAN_POINT ( 'NONE',  ( -30.48921356237309510, -27.52281430457076894, 5.000000000000000000 ) ) ;
#50894=CARTESIAN_POINT ( 'NONE',  ( -32.99999999999976552, -3.033600742197708477, 5.000000000000000000 ) ) ;
#50898=EDGE_CURVE ( 'NONE', #131955, #73568, #114139, .T. ) ;
#50899=VECTOR ( 'NONE', #8151, 1000.000000000000000 ) ;
#50901=ORIENTED_EDGE ( 'NONE', *, *, #105018, .F. ) ;
#50902=DIRECTION ( 'NONE',  ( -0.000000000000000000, 0.000000000000000000, 1.000000000000000000 ) ) ;
#50903=CARTESIAN_POINT ( 'NONE',  ( -22.49999999999984013, 12.05218569542904561, 5.000000000000000000 ) ) ;
#50904=ORIENTED_EDGE ( 'NONE', *, *, #970, .F. ) ;
#50905=ORIENTED_EDGE ( 'NONE', *, *, #102951, .F. ) ;
#50907=VECTOR ( 'NONE', #44343, 1000.000000000000000 ) ;
#50908=CARTESIAN_POINT ( 'NONE',  ( 10.49999999999992539, -14.56887692260766087, 4.000000000000000000 ) ) ;
#50909=ORIENTED_EDGE ( 'NONE', *, *, #8467, .T. ) ;
#50910=DIRECTION ( 'NONE',  ( -0.7071067811865487940, 0.7071067811865463515, -0.000000000000000000 ) ) ;
#50911=ORIENTED_EDGE ( 'NONE', *, *, #59423, .T. ) ;
#50912=CARTESIAN_POINT ( 'NONE',  ( 2.292893218813443657, -3.740707523384248390, 5.000000000000000000 ) ) ;
#50913=EDGE_CURVE ( 'NONE', #127807, #7538, #4596, .T. ) ;
#50914=DIRECTION ( 'NONE',  ( -0.7071067811865486830, -0.7071067811865464625, 0.000000000000000000 ) ) ;
#50915=VECTOR ( 'NONE', #43923, 999.9999999999998863 ) ;
#50916=VECTOR ( 'NONE', #72645, 999.9999999999998863 ) ;
#50917=DIRECTION ( 'NONE',  ( -0.3543493200069163240, -0.000000000000000000, 0.9351131265310288487 ) ) ;
#50918=AXIS2_PLACEMENT_3D ( 'NONE', #115870, #17976, #17296 ) ;
#50919=FACE_BOUND ( 'NONE', #31345, .T. ) ;
#50920=PLANE ( 'NONE',  #78087 ) ;
#50922=DIRECTION ( 'NONE',  ( -0.6830127018922181881, 0.6830127018922202975, -0.2588190451025214056 ) ) ;
#50923=CARTESIAN_POINT ( 'NONE',  ( 34.42499999999998295, 10.54139925780192932, 5.000000000000000000 ) ) ;
#50926=CARTESIAN_POINT ( 'NONE',  ( -9.299744871391588674, -27.71228299555212971, 4.000000000000000000 ) ) ;
#50927=ORIENTED_EDGE ( 'NONE', *, *, #114096, .F. ) ;
#50928=VECTOR ( 'NONE', #79968, 1000.000000000000000 ) ;
#50929=EDGE_LOOP ( 'NONE', ( #94784, #98258, #59238, #121914 ) ) ;
#50931=EDGE_CURVE ( 'NONE', #118585, #10464, #127148, .T. ) ;
#50932=ORIENTED_EDGE ( 'NONE', *, *, #53683, .T. ) ;
#50934=VERTEX_POINT ( 'NONE', #92366 ) ;
#50935=FACE_OUTER_BOUND ( 'NONE', #26851, .T. ) ;
#50937=EDGE_CURVE ( 'NONE', #48062, #48429, #5356, .T. ) ;
#50939=CARTESIAN_POINT ( 'NONE',  ( 36.18398860626899705, 28.73617430169812437, 5.000000000000000000 ) ) ;
#50940=VECTOR ( 'NONE', #119113, 1000.000000000000000 ) ;
#50942=ADVANCED_FACE ( 'NONE', ( #94513 ), #48905, .T. ) ;
#50944=DIRECTION ( 'NONE',  ( 0.6830127018922180770, -0.6830127018922204085, -0.2588190451025213501 ) ) ;
#50945=CARTESIAN_POINT ( 'NONE',  ( -15.18398860626900237, 28.73617430169797871, 5.000000000000000000 ) ) ;
#50946=CARTESIAN_POINT ( 'NONE',  ( 11.20710678118646975, 3.759292476615673007, 5.000000000000000000 ) ) ;
#50947=ORIENTED_EDGE ( 'NONE', *, *, #18036, .F. ) ;
#50949=ORIENTED_EDGE ( 'NONE', *, *, #33574, .F. ) ;
#50950=CARTESIAN_POINT ( 'NONE',  ( -3.183988606268992161, 28.73617430169789699, 5.000000000000000000 ) ) ;
#50952=ORIENTED_EDGE ( 'NONE', *, *, #134100, .T. ) ;
#50954=ORIENTED_EDGE ( 'NONE', *, *, #102262, .F. ) ;
#50955=LINE ( 'NONE', #68615, #134637 ) ;
#50956=EDGE_CURVE ( 'NONE', #488, #37639, #6755, .T. ) ;
#50957=FACE_OUTER_BOUND ( 'NONE', #102044, .T. ) ;
#50958=ORIENTED_EDGE ( 'NONE', *, *, #87813, .T. ) ;
#50959=CARTESIAN_POINT ( 'NONE',  ( 25.73493329717933875, 12.75929247661558996, 18.34774599283950280 ) ) ;
#50960=CARTESIAN_POINT ( 'NONE',  ( -34.92500000000001137, -22.22500000000000142, 4.500000000000000888 ) ) ;
#50963=ORIENTED_EDGE ( 'NONE', *, *, #79615, .T. ) ;
#50965=CARTESIAN_POINT ( 'NONE',  ( 17.99999999999987566, -7.068876922607736368, 4.000000000000000000 ) ) ;
#50966=CARTESIAN_POINT ( 'NONE',  ( 0.000000000000000000, 0.000000000000000000, 5.000000000000000000 ) ) ;
#50967=CARTESIAN_POINT ( 'NONE',  ( -9.489213562373095101, -27.52281430457062328, 5.000000000000000000 ) ) ;
#50969=LINE ( 'NONE', #16149, #23964 ) ;
#50970=ORIENTED_EDGE ( 'NONE', *, *, #9053, .T. ) ;
#50971=LINE ( 'NONE', #95167, #56546 ) ;
#50972=PLANE ( 'NONE',  #5290 ) ;
#50974=ORIENTED_EDGE ( 'NONE', *, *, #90496, .F. ) ;
#50975=AXIS2_PLACEMENT_3D ( 'NONE', #55612, #31011, #109968 ) ;
#50977=LINE ( 'NONE', #93046, #12411 ) ;
#50978=PLANE ( 'NONE',  #115807 ) ;
#50979=FACE_OUTER_BOUND ( 'NONE', #54327, .T. ) ;
#50980=VECTOR ( 'NONE', #51064, 1000.000000000000000 ) ;
#50981=EDGE_LOOP ( 'NONE', ( #127860, #109657, #135244, #78052 ) ) ;
#50982=VECTOR ( 'NONE', #127443, 999.9999999999998863 ) ;
#50983=VECTOR ( 'NONE', #108716, 1000.000000000000000 ) ;
#50985=PLANE ( 'NONE',  #62493 ) ;
#50986=DIRECTION ( 'NONE',  ( -0.7071067811865486830, 0.7071067811865464625, 0.000000000000000000 ) ) ;
#50987=CARTESIAN_POINT ( 'NONE',  ( -24.18398860626899705, 28.73617430169804265, 5.000000000000000000 ) ) ;
#50988=VECTOR ( 'NONE', #33495, 1000.000000000000000 ) ;
#50990=DIRECTION ( 'NONE',  ( -0.7071067811865486830, 0.7071067811865464625, 0.000000000000000000 ) ) ;
#50991=ORIENTED_EDGE ( 'NONE', *, *, #116443, .F. ) ;
#50992=EDGE_CURVE ( 'NONE', #103755, #122142, #141617, .T. ) ;
#50993=ORIENTED_EDGE ( 'NONE', *, *, #21883, .T. ) ;
#50994=DIRECTION ( 'NONE',  ( 0.7071067811865487940, 0.7071067811865463515, -0.000000000000000000 ) ) ;
#50995=AXIS2_PLACEMENT_3D ( 'NONE', #62451, #69225, #124300 ) ;
#50998=DIRECTION ( 'NONE',  ( -0.6830127018922181881, 0.6830127018922202975, -0.2588190451025214056 ) ) ;
#51000=DIRECTION ( 'NONE',  ( -0.7071067811865486830, -0.7071067811865464625, 0.000000000000000000 ) ) ;
#51002=PLANE ( 'NONE',  #37254 ) ;
#51003=LINE ( 'NONE', #80959, #283 ) ;
#51004=CARTESIAN_POINT ( 'NONE',  ( 34.49999999999976552, 6.277155672890305738, -3.510561720659021834 ) ) ;
#51005=VECTOR ( 'NONE', #117283, 1000.000000000000000 ) ;
#51006=CARTESIAN_POINT ( 'NONE',  ( -6.792893218813411238, 6.759292476615643253, 5.000000000000000000 ) ) ;
#51008=DIRECTION ( 'NONE',  ( 1.000000000000000000, 0.000000000000000000, 0.000000000000000000 ) ) ;
#51009=EDGE_LOOP ( 'NONE', ( #84841, #3914, #127666, #42772 ) ) ;
#51010=CARTESIAN_POINT ( 'NONE',  ( -8.483345613589495571, 22.22500000000000142, 4.500000000000000888 ) ) ;
#51011=VECTOR ( 'NONE', #88568, 1000.000000000000227 ) ;
#51014=ORIENTED_EDGE ( 'NONE', *, *, #17406, .F. ) ;
#51015=LINE ( 'NONE', #6730, #40816 ) ;
#51016=VECTOR ( 'NONE', #59920, 999.9999999999998863 ) ;
#51017=DIRECTION ( 'NONE',  ( 0.6830127018922180770, -0.6830127018922204085, -0.2588190451025213501 ) ) ;
#51019=PLANE ( 'NONE',  #92608 ) ;
#51021=CARTESIAN_POINT ( 'NONE',  ( -18.48921356237309510, -27.52281430457068367, 5.000000000000000000 ) ) ;
#51022=VECTOR ( 'NONE', #49767, 999.9999999999998863 ) ;
#51023=ORIENTED_EDGE ( 'NONE', *, *, #130953, .T. ) ;
#51025=DIRECTION ( 'NONE',  ( -0.7071067811865486830, 0.7071067811865464625, 0.000000000000000000 ) ) ;
#51026=CARTESIAN_POINT ( 'NONE',  ( -31.49999999999977973, -5.947814304570768762, 5.000000000000000000 ) ) ;
#51028=CARTESIAN_POINT ( 'NONE',  ( -39.48921356237310221, -27.52281430457082934, 5.000000000000000000 ) ) ;
#51029=CARTESIAN_POINT ( 'NONE',  ( -9.299744871391588674, -27.71228299555212971, 4.000000000000000000 ) ) ;
#51034=EDGE_LOOP ( 'NONE', ( #79628, #35593, #135413, #141568 ) ) ;
#51037=FACE_OUTER_BOUND ( 'NONE', #132874, .T. ) ;
#51038=ADVANCED_FACE ( 'NONE', ( #96631 ), #41568, .F. ) ;
#51039=DIRECTION ( 'NONE',  ( -0.7071067811865486830, -0.7071067811865464625, 0.000000000000000000 ) ) ;
#51040=EDGE_CURVE ( 'NONE', #37517, #109570, #65514, .T. ) ;
#51041=VECTOR ( 'NONE', #137700, 1000.000000000000000 ) ;
#51042=DIRECTION ( 'NONE',  ( 0.6830127018922180770, -0.6830127018922204085, -0.2588190451025213501 ) ) ;
#51044=EDGE_CURVE ( 'NONE', #140231, #31707, #131456, .T. ) ;
#51045=CARTESIAN_POINT ( 'NONE',  ( -3.328169399223505742, -15.74070752338412049, 4.000000000000000000 ) ) ;
#51047=ORIENTED_EDGE ( 'NONE', *, *, #8711, .F. ) ;
#51048=LINE ( 'NONE', #50335, #64157 ) ;
#51049=ORIENTED_EDGE ( 'NONE', *, *, #53665, .T. ) ;
#51050=VERTEX_POINT ( 'NONE', #53917 ) ;
#51051=AXIS2_PLACEMENT_3D ( 'NONE', #65972, #78256, #45639 ) ;
#51055=EDGE_CURVE ( 'NONE', #39646, #40495, #64768, .T. ) ;
#51057=EDGE_CURVE ( 'NONE', #7970, #10035, #34682, .T. ) ;
#51058=DIRECTION ( 'NONE',  ( -0.7071067811865486830, -0.7071067811865464625, 0.000000000000000000 ) ) ;
#51060=ORIENTED_EDGE ( 'NONE', *, *, #52756, .T. ) ;
#51061=DIRECTION ( 'NONE',  ( -0.000000000000000000, 0.3543493200069153248, 0.9351131265310292928 ) ) ;
#51062=CARTESIAN_POINT ( 'NONE',  ( -12.32816939922344623, 11.25929247661559884, 4.000000000000000000 ) ) ;
#51063=CARTESIAN_POINT ( 'NONE',  ( -12.32816939922343913, 17.25929247661554200, 4.000000000000000000 ) ) ;
#51064=DIRECTION ( 'NONE',  ( 0.7071067811865486830, -0.7071067811865464625, -0.000000000000000000 ) ) ;
#51065=DIRECTION ( 'NONE',  ( 0.7071067811865487940, 0.7071067811865463515, 0.000000000000000000 ) ) ;
#51068=ADVANCED_FACE ( 'NONE', ( #9639 ), #21253, .F. ) ;
#51069=ORIENTED_EDGE ( 'NONE', *, *, #87193, .T. ) ;
#51070=ORIENTED_EDGE ( 'NONE', *, *, #113244, .F. ) ;
#51073=LINE ( 'NONE', #72144, #139035 ) ;
#51074=CARTESIAN_POINT ( 'NONE',  ( 6.618384906019920244, -2.240707523384264377, 13.37739548510237952 ) ) ;
#51076=EDGE_LOOP ( 'NONE', ( #1321, #40973, #15121, #131205 ) ) ;
#51077=ORIENTED_EDGE ( 'NONE', *, *, #78197, .F. ) ;
#51078=EDGE_CURVE ( 'NONE', #37121, #32625, #30728, .T. ) ;
#51079=CARTESIAN_POINT ( 'NONE',  ( 30.18398860626900060, 28.73617430169808173, 5.000000000000000000 ) ) ;
#51081=VECTOR ( 'NONE', #57621, 999.9999999999998863 ) ;
#51082=ORIENTED_EDGE ( 'NONE', *, *, #54596, .F. ) ;
#51083=VECTOR ( 'NONE', #73064, 1000.000000000000227 ) ;
#51084=VECTOR ( 'NONE', #40220, 1000.000000000000000 ) ;
#51085=ORIENTED_EDGE ( 'NONE', *, *, #49978, .T. ) ;
#51086=CARTESIAN_POINT ( 'NONE',  ( 5.999999999999956479, -0.2811185226894233335, -5.995736974527527074 ) ) ;
#51087=ORIENTED_EDGE ( 'NONE', *, *, #45197, .F. ) ;
#51089=EDGE_CURVE ( 'NONE', #132586, #24733, #8884, .T. ) ;
#51090=VECTOR ( 'NONE', #88614, 1000.000000000000000 ) ;
#51091=AXIS2_PLACEMENT_3D ( 'NONE', #43336, #141956, #75958 ) ;
#51092=AXIS2_PLACEMENT_3D ( 'NONE', #59225, #70111, #91797 ) ;
#51093=AXIS2_PLACEMENT_3D ( 'NONE', #117974, #121398, #7808 ) ;
#51094=VECTOR ( 'NONE', #73601, 1000.000000000000227 ) ;
#51095=FACE_BOUND ( 'NONE', #92668, .T. ) ;
#51096=CARTESIAN_POINT ( 'NONE',  ( -34.92500000000001137, 11.81665438641030441, 4.500000000000000888 ) ) ;
#51098=AXIS2_PLACEMENT_3D ( 'NONE', #50847, #28389, #40691 ) ;
#51099=LINE ( 'NONE', #32189, #17849 ) ;
#51100=LINE ( 'NONE', #117729, #18033 ) ;
#51101=ORIENTED_EDGE ( 'NONE', *, *, #33672, .F. ) ;
#51102=DIRECTION ( 'NONE',  ( 0.7071067811865487940, 0.7071067811865463515, 0.000000000000000000 ) ) ;
#51104=ADVANCED_FACE ( 'NONE', ( #109691 ), #10359, .F. ) ;
#51105=ORIENTED_EDGE ( 'NONE', *, *, #7766, .T. ) ;
#51106=VERTEX_POINT ( 'NONE', #143035 ) ;
#51108=ORIENTED_EDGE ( 'NONE', *, *, #127353, .F. ) ;
#51109=DIRECTION ( 'NONE',  ( 0.7071067811865487940, 0.7071067811865463515, 0.000000000000000000 ) ) ;
#51110=AXIS2_PLACEMENT_3D ( 'NONE', #114284, #27261, #4750 ) ;
#51111=CARTESIAN_POINT ( 'NONE',  ( 11.99451991528749417, 28.92564299267946382, 4.000000000000000000 ) ) ;
#51112=CARTESIAN_POINT ( 'NONE',  ( -34.92500000000001137, -0.8020632299005174826, 13.72581505463524998 ) ) ;
#51113=ORIENTED_EDGE ( 'NONE', *, *, #49876, .T. ) ;
#51114=DIRECTION ( 'NONE',  ( -1.000000000000000000, 0.000000000000000000, 0.000000000000000000 ) ) ;
#51115=VECTOR ( 'NONE', #31319, 1000.000000000000000 ) ;
#51117=ADVANCED_FACE ( 'NONE', ( #76360 ), #43721, .T. ) ;
#51118=CARTESIAN_POINT ( 'NONE',  ( -54.48921356237310221, -27.52281430457093236, 5.000000000000000000 ) ) ;
#51119=CARTESIAN_POINT ( 'NONE',  ( -57.18398860626899705, 28.73617430169827358, 5.000000000000000000 ) ) ;
#51120=VECTOR ( 'NONE', #31252, 1000.000000000000000 ) ;
#51121=FACE_OUTER_BOUND ( 'NONE', #50084, .T. ) ;
#51122=CARTESIAN_POINT ( 'NONE',  ( -28.49999999999979750, -10.91253812416064406, 4.000000000000000000 ) ) ;
#51125=CARTESIAN_POINT ( 'NONE',  ( 12.48921356237309155, -27.52281430457064104, 5.000000000000000000 ) ) ;
#51126=LINE ( 'NONE', #73584, #111375 ) ;
#51127=ORIENTED_EDGE ( 'NONE', *, *, #83440, .F. ) ;
#51128=ORIENTED_EDGE ( 'NONE', *, *, #20363, .T. ) ;
#51129=EDGE_CURVE ( 'NONE', #138233, #1245, #97355, .T. ) ;
#51130=VECTOR ( 'NONE', #130890, 999.9999999999998863 ) ;
#51131=EDGE_LOOP ( 'NONE', ( #74335, #110843, #56307, #100635 ) ) ;
#51133=VERTEX_POINT ( 'NONE', #18358 ) ;
#51136=ORIENTED_EDGE ( 'NONE', *, *, #38949, .F. ) ;
#51137=DIRECTION ( 'NONE',  ( 0.6830127018922180770, -0.6830127018922204085, -0.2588190451025213501 ) ) ;
#51138=ORIENTED_EDGE ( 'NONE', *, *, #60669, .F. ) ;
#51139=CARTESIAN_POINT ( 'NONE',  ( 18.77004279457781166, 21.73644205237998506, 5.000000000000000888 ) ) ;
#51140=AXIS2_PLACEMENT_3D ( 'NONE', #66032, #76174, #44276 ) ;
#51141=LINE ( 'NONE', #71460, #133104 ) ;
#51142=DIRECTION ( 'NONE',  ( 0.7071067811865486830, -0.7071067811865464625, -0.000000000000000000 ) ) ;
#51144=ORIENTED_EDGE ( 'NONE', *, *, #37929, .T. ) ;
#51146=VERTEX_POINT ( 'NONE', #140188 ) ;
#51147=CARTESIAN_POINT ( 'NONE',  ( 11.99451991528749417, 28.92564299267946382, 4.000000000000000000 ) ) ;
#51148=EDGE_LOOP ( 'NONE', ( #36599, #9270, #121779, #113828 ) ) ;
#51149=EDGE_CURVE ( 'NONE', #89715, #87848, #40875, .T. ) ;
#51150=ORIENTED_EDGE ( 'NONE', *, *, #30909, .T. ) ;
#51151=ORIENTED_EDGE ( 'NONE', *, *, #87211, .T. ) ;
#51152=VERTEX_POINT ( 'NONE', #62634 ) ;
#51154=VECTOR ( 'NONE', #16525, 1000.000000000000000 ) ;
#51156=DIRECTION ( 'NONE',  ( -0.7071067811865486830, -0.7071067811865464625, 0.000000000000000000 ) ) ;
#51157=EDGE_CURVE ( 'NONE', #59760, #81280, #7503, .T. ) ;
#51158=CARTESIAN_POINT ( 'NONE',  ( -28.49999999999980460, -16.91253812416058366, 4.000000000000000000 ) ) ;
#51159=ORIENTED_EDGE ( 'NONE', *, *, #80067, .T. ) ;
#51160=EDGE_CURVE ( 'NONE', #110495, #92174, #51763, .T. ) ;
#51161=CARTESIAN_POINT ( 'NONE',  ( 38.99451991528749062, 28.92564299267965211, 4.000000000000000000 ) ) ;
#51164=DIRECTION ( 'NONE',  ( -0.7071067811865487940, 0.7071067811865463515, -0.000000000000000000 ) ) ;
#51165=FACE_OUTER_BOUND ( 'NONE', #35475, .T. ) ;
#51166=CARTESIAN_POINT ( 'NONE',  ( 4.499999999999968914, -4.216083040037243101, -7.486842126848666901 ) ) ;
#51167=VERTEX_POINT ( 'NONE', #107542 ) ;
#51168=DIRECTION ( 'NONE',  ( 1.000000000000000000, 0.000000000000000000, 0.000000000000000000 ) ) ;
#51169=DIRECTION ( 'NONE',  ( 0.6830127018922180770, -0.6830127018922204085, -0.2588190451025213501 ) ) ;
#51170=ORIENTED_EDGE ( 'NONE', *, *, #122326, .F. ) ;
#51172=ORIENTED_EDGE ( 'NONE', *, *, #90182, .F. ) ;
#51173=CARTESIAN_POINT ( 'NONE',  ( 3.489213562373097322, -27.52281430457057709, 5.000000000000000000 ) ) ;
#51174=DIRECTION ( 'NONE',  ( 0.7071067811865486830, -0.7071067811865464625, -0.000000000000000000 ) ) ;
#51176=VECTOR ( 'NONE', #133358, 999.9999999999998863 ) ;
#51180=CARTESIAN_POINT ( 'NONE',  ( 23.29289321881329755, 17.25929247661554911, 5.000000000000000000 ) ) ;
#51182=VECTOR ( 'NONE', #114006, 1000.000000000000000 ) ;
#51183=DIRECTION ( 'NONE',  ( -0.000000000000000000, 0.3543493200069153248, 0.9351131265310292928 ) ) ;
#51184=CARTESIAN_POINT ( 'NONE',  ( -29.99999999999979039, 7.588810512006185505, -3.013526669885157716 ) ) ;
#51187=ORIENTED_EDGE ( 'NONE', *, *, #88492, .F. ) ;
#51188=AXIS2_PLACEMENT_3D ( 'NONE', #49579, #114083, #38672 ) ;
#51189=VECTOR ( 'NONE', #87915, 999.9999999999998863 ) ;
#51190=AXIS2_PLACEMENT_3D ( 'NONE', #38515, #126921, #6538 ) ;
#51192=FACE_OUTER_BOUND ( 'NONE', #29600, .T. ) ;
#51193=EDGE_LOOP ( 'NONE', ( #127031, #111196, #55186, #20035 ) ) ;
#51195=LINE ( 'NONE', #51913, #122395 ) ;
#51196=DIRECTION ( 'NONE',  ( 0.3543493200069162685, -0.000000000000000000, -0.9351131265310288487 ) ) ;
#51197=ORIENTED_EDGE ( 'NONE', *, *, #125327, .T. ) ;
#51198=CARTESIAN_POINT ( 'NONE',  ( 20.99999999999985079, 7.007997736742463957, -8.085015511992065029 ) ) ;
#51199=FACE_OUTER_BOUND ( 'NONE', #81914, .T. ) ;
#51200=EDGE_LOOP ( 'NONE', ( #98466, #52991, #68428 ) ) ;
#51201=ORIENTED_EDGE ( 'NONE', *, *, #27513, .T. ) ;
#51202=DIRECTION ( 'NONE',  ( 1.000000000000000000, -0.000000000000000000, 0.000000000000000000 ) ) ;
#51203=DIRECTION ( 'NONE',  ( 0.3543493200069162685, -0.000000000000000000, -0.9351131265310288487 ) ) ;
#51204=VECTOR ( 'NONE', #75141, 999.9999999999998863 ) ;
#51205=LINE ( 'NONE', #75117, #114705 ) ;
#51207=LINE ( 'NONE', #30891, #99488 ) ;
#51208=EDGE_CURVE ( 'NONE', #37388, #100143, #121972, .T. ) ;
#51209=CARTESIAN_POINT ( 'NONE',  ( 7.828169399223469327, -17.24070752338410628, 4.000000000000000000 ) ) ;
#51210=ORIENTED_EDGE ( 'NONE', *, *, #103694, .T. ) ;
#51211=CARTESIAN_POINT ( 'NONE',  ( -8.207106781186482181, -17.24070752338409918, 5.000000000000000000 ) ) ;
#51212=ADVANCED_FACE ( 'NONE', ( #2321 ), #1607, .F. ) ;
#51213=CARTESIAN_POINT ( 'NONE',  ( -45.29974487139158867, -27.71228299555237840, 4.000000000000000000 ) ) ;
#51215=VECTOR ( 'NONE', #30510, 1000.000000000000000 ) ;
#51217=ORIENTED_EDGE ( 'NONE', *, *, #96986, .T. ) ;
#51219=EDGE_CURVE ( 'NONE', #113826, #139855, #46640, .T. ) ;
#51221=LINE ( 'NONE', #16401, #441 ) ;
#51222=ORIENTED_EDGE ( 'NONE', *, *, #25782, .T. ) ;
#51223=VECTOR ( 'NONE', #10378, 1000.000000000000227 ) ;
#51225=VECTOR ( 'NONE', #86067, 999.9999999999998863 ) ;
#51226=DIRECTION ( 'NONE',  ( 1.000000000000000000, 0.000000000000000000, 0.000000000000000000 ) ) ;
#51227=CARTESIAN_POINT ( 'NONE',  ( 4.499999999999966249, 9.431123077392086884, 4.000000000000000000 ) ) ;
#51228=CARTESIAN_POINT ( 'NONE',  ( 6.183988606268994381, 28.73617430169791476, 5.000000000000000000 ) ) ;
#51229=ORIENTED_EDGE ( 'NONE', *, *, #22626, .T. ) ;
#51231=CARTESIAN_POINT ( 'NONE',  ( 25.63753812416080180, 22.22500000000000142, 4.000000000000000000 ) ) ;
#51232=CARTESIAN_POINT ( 'NONE',  ( -39.18398860626899705, 28.73617430169814568, 5.000000000000000000 ) ) ;
#51235=VECTOR ( 'NONE', #112506, 1000.000000000000000 ) ;
#51236=EDGE_CURVE ( 'NONE', #4967, #68187, #33710, .T. ) ;
#51237=CARTESIAN_POINT ( 'NONE',  ( 18.48921356237309510, -27.52281430457068367, 5.000000000000000000 ) ) ;
#51238=ORIENTED_EDGE ( 'NONE', *, *, #82807, .F. ) ;
#51239=LINE ( 'NONE', #49104, #83099 ) ;
#51240=LINE ( 'NONE', #128777, #89288 ) ;
#51241=CARTESIAN_POINT ( 'NONE',  ( 17.18753812416040461, -22.22500000000000142, 4.000000000000000000 ) ) ;
#51242=DIRECTION ( 'NONE',  ( -0.000000000000000000, -0.3543493200069152693, 0.9351131265310292928 ) ) ;
#51243=ORIENTED_EDGE ( 'NONE', *, *, #21463, .T. ) ;
#51244=ORIENTED_EDGE ( 'NONE', *, *, #123501, .F. ) ;
#51246=VECTOR ( 'NONE', #117199, 999.9999999999998863 ) ;
#51247=VERTEX_POINT ( 'NONE', #907 ) ;
#51248=EDGE_CURVE ( 'NONE', #48427, #76949, #135055, .T. ) ;
#51249=AXIS2_PLACEMENT_3D ( 'NONE', #42510, #88136, #64237 ) ;
#51250=CARTESIAN_POINT ( 'NONE',  ( 72.29974487139158157, -27.71228299555256669, 4.000000000000000000 ) ) ;
#51251=FACE_OUTER_BOUND ( 'NONE', #95597, .T. ) ;
#51252=EDGE_LOOP ( 'NONE', ( #23498, #68962, #47622, #77817 ) ) ;
#51253=EDGE_CURVE ( 'NONE', #15605, #128738, #90065, .T. ) ;
#51254=VECTOR ( 'NONE', #128204, 1000.000000000000000 ) ;
#51257=ORIENTED_EDGE ( 'NONE', *, *, #81474, .T. ) ;
#51258=CARTESIAN_POINT ( 'NONE',  ( 17.11087965568911073, 8.820243421702873121, 4.000000000000000000 ) ) ;
#51260=ADVANCED_FACE ( 'NONE', ( #13923 ), #89369, .F. ) ;
#51261=CARTESIAN_POINT ( 'NONE',  ( 5.999999999999981348, 20.58746187583903620, 4.000000000000000000 ) ) ;
#51262=AXIS2_PLACEMENT_3D ( 'NONE', #44230, #33377, #89151 ) ;
#51263=VERTEX_POINT ( 'NONE', #99501 ) ;
#51264=ORIENTED_EDGE ( 'NONE', *, *, #57602, .F. ) ;
#51265=FACE_OUTER_BOUND ( 'NONE', #73750, .T. ) ;
#51266=PLANE ( 'NONE',  #53120 ) ;
#51267=EDGE_CURVE ( 'NONE', #3592, #270, #45190, .T. ) ;
#51268=CARTESIAN_POINT ( 'NONE',  ( 65.99451991528749772, 28.92564299267984396, 4.000000000000000000 ) ) ;
#51269=LINE ( 'NONE', #94731, #51295 ) ;
#51270=ADVANCED_FACE ( 'NONE', ( #35016 ), #132179, .F. ) ;
#51271=VECTOR ( 'NONE', #8025, 1000.000000000000000 ) ;
#51273=DIRECTION ( 'NONE',  ( 0.7071067811865487940, 0.7071067811865463515, 0.000000000000000000 ) ) ;
#51275=EDGE_CURVE ( 'NONE', #109227, #56761, #111847, .T. ) ;
#51276=ORIENTED_EDGE ( 'NONE', *, *, #143334, .T. ) ;
#51279=VERTEX_POINT ( 'NONE', #78499 ) ;
#51281=EDGE_CURVE ( 'NONE', #17061, #136777, #100949, .T. ) ;
#51282=( BOUNDED_CURVE ( )  B_SPLINE_CURVE ( 3, ( #85220, #140333, #84544, #7657 ),
 .UNSPECIFIED., .F., .F. ) 
 B_SPLINE_CURVE_WITH_KNOTS ( ( 4, 4 ),
 ( 2.779374508378134045, 4.199602562396879790 ),
 .UNSPECIFIED. ) 
 CURVE ( )  GEOMETRIC_REPRESENTATION_ITEM ( )  RATIONAL_B_SPLINE_CURVE ( ( 1.000000000000000000, 0.8388583629366537231, 0.8388583629366537231, 1.000000000000000000 ) ) 
 REPRESENTATION_ITEM ( '' )  );
#51283=AXIS2_PLACEMENT_3D ( 'NONE', #129506, #9878, #98338 ) ;
#51284=LINE ( 'NONE', #128820, #52046 ) ;
#51286=CARTESIAN_POINT ( 'NONE',  ( 9.183988606268997046, 28.73617430169793607, 5.000000000000000000 ) ) ;
#51287=CARTESIAN_POINT ( 'NONE',  ( 25.49999999999982947, -9.462702396500981550, -9.474982329943568260 ) ) ;
#51289=FACE_OUTER_BOUND ( 'NONE', #89440, .T. ) ;
#51290=VECTOR ( 'NONE', #22421, 1000.000000000000000 ) ;
#51291=AXIS2_PLACEMENT_3D ( 'NONE', #46984, #135389, #4785 ) ;
#51292=AXIS2_PLACEMENT_3D ( 'NONE', #70989, #42650, #84698 ) ;
#51293=DIRECTION ( 'NONE',  ( 4.681814790819592407E-17, 0.3543493200069153248, 0.9351131265310292928 ) ) ;
#51295=VECTOR ( 'NONE', #72344, 1000.000000000000000 ) ;
#51296=CARTESIAN_POINT ( 'NONE',  ( -3.489213562373097322, -27.52281430457057709, 5.000000000000000000 ) ) ;
#51297=EDGE_LOOP ( 'NONE', ( #79096, #27052, #84270, #82712 ) ) ;
#51298=CARTESIAN_POINT ( 'NONE',  ( 78.29974487139158157, -27.71228299555260577, 4.000000000000000000 ) ) ;
#51299=ORIENTED_EDGE ( 'NONE', *, *, #35551, .F. ) ;
#51301=ORIENTED_EDGE ( 'NONE', *, *, #63681, .F. ) ;
#51302=AXIS2_PLACEMENT_3D ( 'NONE', #11795, #98813, #143047 ) ;
#51305=PLANE ( 'NONE',  #34987 ) ;
#51306=CARTESIAN_POINT ( 'NONE',  ( 63.18398860626900415, 28.73617430169831621, 5.000000000000000000 ) ) ;
#51308=PLANE ( 'NONE',  #7763 ) ;
#51310=LINE ( 'NONE', #63635, #37104 ) ;
#51311=DIRECTION ( 'NONE',  ( -0.6830127018922181881, 0.6830127018922202975, -0.2588190451025214056 ) ) ;
#51312=LINE ( 'NONE', #7770, #130376 ) ;
#51314=VECTOR ( 'NONE', #131870, 999.9999999999998863 ) ;
#51315=DIRECTION ( 'NONE',  ( 0.3543493200069162685, -0.000000000000000000, -0.9351131265310288487 ) ) ;
#51316=ORIENTED_EDGE ( 'NONE', *, *, #122558, .F. ) ;
#51317=VECTOR ( 'NONE', #38235, 1000.000000000000000 ) ;
#51318=CARTESIAN_POINT ( 'NONE',  ( -51.29974487139158867, -27.71228299555242103, 4.000000000000000000 ) ) ;
#51320=ORIENTED_EDGE ( 'NONE', *, *, #21388, .T. ) ;
#51321=VECTOR ( 'NONE', #92836, 999.9999999999998863 ) ;
#51322=ORIENTED_EDGE ( 'NONE', *, *, #129421, .F. ) ;
#51323=DIRECTION ( 'NONE',  ( -0.6830127018922180770, -0.6830127018922204085, -0.2588190451025213501 ) ) ;
#51324=ORIENTED_EDGE ( 'NONE', *, *, #67832, .T. ) ;
#51325=VECTOR ( 'NONE', #88294, 1000.000000000000000 ) ;
#51327=LINE ( 'NONE', #129571, #31595 ) ;
#51328=ADVANCED_FACE ( 'NONE', ( #22643 ), #77792, .T. ) ;
#51329=LINE ( 'NONE', #83981, #120464 ) ;
#51330=ORIENTED_EDGE ( 'NONE', *, *, #46123, .T. ) ;
#51331=ADVANCED_FACE ( 'NONE', ( #23382 ), #67654, .T. ) ;
#51333=ORIENTED_EDGE ( 'NONE', *, *, #10713, .F. ) ;
#51334=AXIS2_PLACEMENT_3D ( 'NONE', #40252, #29329, #51828 ) ;
#51336=FACE_OUTER_BOUND ( 'NONE', #142766, .T. ) ;
#51337=CARTESIAN_POINT ( 'NONE',  ( 0.000000000000000000, 0.000000000000000000, 5.000000000000000000 ) ) ;
#51338=EDGE_CURVE ( 'NONE', #82669, #80263, #137169, .T. ) ;
#51339=FACE_OUTER_BOUND ( 'NONE', #137728, .T. ) ;
#51340=ORIENTED_EDGE ( 'NONE', *, *, #3658, .F. ) ;
#51343=ORIENTED_EDGE ( 'NONE', *, *, #134041, .F. ) ;
#51344=CARTESIAN_POINT ( 'NONE',  ( 21.18398860626899349, 28.73617430169802134, 5.000000000000000000 ) ) ;
#51346=CARTESIAN_POINT ( 'NONE',  ( 6.005480084712508493, 28.92564299267933947, 4.000000000000000000 ) ) ;
#51347=AXIS2_PLACEMENT_3D ( 'NONE', #107507, #64019, #140832 ) ;
#51348=CARTESIAN_POINT ( 'NONE',  ( -45.29974487139158867, -27.71228299555237840, 4.000000000000000000 ) ) ;
#51349=LINE ( 'NONE', #9200, #62175 ) ;
#51351=EDGE_CURVE ( 'NONE', #83817, #137730, #124850, .T. ) ;
#51352=DIRECTION ( 'NONE',  ( -0.7071067811865486830, 0.7071067811865464625, 0.000000000000000000 ) ) ;
#51353=DIRECTION ( 'NONE',  ( -0.7071067811865486830, 0.7071067811865464625, 0.000000000000000000 ) ) ;
#51355=VECTOR ( 'NONE', #30249, 1000.000000000000000 ) ;
#51356=ORIENTED_EDGE ( 'NONE', *, *, #88197, .T. ) ;
#51358=AXIS2_PLACEMENT_3D ( 'NONE', #127090, #7437, #51702 ) ;
#51359=EDGE_CURVE ( 'NONE', #46464, #5794, #82794, .T. ) ;
#51360=DIRECTION ( 'NONE',  ( 0.6830127018922180770, -0.6830127018922204085, -0.2588190451025213501 ) ) ;
#51361=ORIENTED_EDGE ( 'NONE', *, *, #5307, .F. ) ;
#51362=DIRECTION ( 'NONE',  ( -0.000000000000000000, -0.3543493200069152693, 0.9351131265310292928 ) ) ;
#51363=DIRECTION ( 'NONE',  ( 0.3543493200069162685, -0.000000000000000000, -0.9351131265310288487 ) ) ;
#51364=ORIENTED_EDGE ( 'NONE', *, *, #113042, .F. ) ;
#51365=CARTESIAN_POINT ( 'NONE',  ( 0.4892135623730947680, -27.52281430457055578, 5.000000000000000000 ) ) ;
#51368=AXIS2_PLACEMENT_3D ( 'NONE', #133770, #58400, #22819 ) ;
#51369=ORIENTED_EDGE ( 'NONE', *, *, #46481, .T. ) ;
#51370=LINE ( 'NONE', #141963, #21157 ) ;
#51371=ORIENTED_EDGE ( 'NONE', *, *, #121037, .F. ) ;
#51373=CARTESIAN_POINT ( 'NONE',  ( 12.70710678118645731, -15.74070752338412049, 5.000000000000000000 ) ) ;
#51374=DIRECTION ( 'NONE',  ( 0.6830127018922181881, 0.6830127018922202975, -0.2588190451025214056 ) ) ;
#51377=CARTESIAN_POINT ( 'NONE',  ( 17.99999999999987210, -13.06887692260767686, 4.000000000000000000 ) ) ;
#51380=VECTOR ( 'NONE', #114107, 1000.000000000000000 ) ;
#51381=VECTOR ( 'NONE', #63976, 999.9999999999998863 ) ;
#51382=CARTESIAN_POINT ( 'NONE',  ( -34.42500000000001137, 16.54139925780184583, 5.000000000000000000 ) ) ;
#51383=DIRECTION ( 'NONE',  ( -0.000000000000000000, -0.3543493200069152693, 0.9351131265310292928 ) ) ;
#51384=ORIENTED_EDGE ( 'NONE', *, *, #108419, .F. ) ;
#51385=ADVANCED_FACE ( 'NONE', ( #49475 ), #16047, .F. ) ;
#51386=ORIENTED_EDGE ( 'NONE', *, *, #45307, .F. ) ;
#51387=VECTOR ( 'NONE', #120431, 1000.000000000000000 ) ;
#51388=EDGE_CURVE ( 'NONE', #103866, #130801, #15342, .T. ) ;
#51392=VERTEX_POINT ( 'NONE', #47358 ) ;
#51394=PLANE ( 'NONE',  #125079 ) ;
#51395=VECTOR ( 'NONE', #111273, 1000.000000000000000 ) ;
#51396=VECTOR ( 'NONE', #86009, 1000.000000000000000 ) ;
#51397=PLANE ( 'NONE',  #110374 ) ;
#51398=EDGE_LOOP ( 'NONE', ( #23144, #110300, #107320, #125286 ) ) ;
#51399=EDGE_CURVE ( 'NONE', #31547, #11149, #127726, .T. ) ;
#51400=PLANE ( 'NONE',  #63 ) ;
#51402=DIRECTION ( 'NONE',  ( 0.7071067811865487940, 0.7071067811865463515, -0.000000000000000000 ) ) ;
#51403=ADVANCED_FACE ( 'NONE', ( #37125 ), #48733, .T. ) ;
#51404=EDGE_CURVE ( 'NONE', #95958, #3113, #38563, .T. ) ;
#51405=LINE ( 'NONE', #72478, #93812 ) ;
#51406=ORIENTED_EDGE ( 'NONE', *, *, #20157, .T. ) ;
#51407=FACE_OUTER_BOUND ( 'NONE', #120599, .T. ) ;
#51408=DIRECTION ( 'NONE',  ( -0.000000000000000000, 0.3543493200069153248, 0.9351131265310292928 ) ) ;
#51409=DIRECTION ( 'NONE',  ( -0.000000000000000000, 0.000000000000000000, 1.000000000000000000 ) ) ;
#51410=CARTESIAN_POINT ( 'NONE',  ( 12.70701326429294831, -21.74070752338406365, 4.999753212805217117 ) ) ;
#51411=CARTESIAN_POINT ( 'NONE',  ( -27.48921356237309155, -27.52281430457074762, 5.000000000000000000 ) ) ;
#51413=ORIENTED_EDGE ( 'NONE', *, *, #73769, .F. ) ;
#51414=VERTEX_POINT ( 'NONE', #93665 ) ;
#51416=ORIENTED_EDGE ( 'NONE', *, *, #102808, .T. ) ;
#51417=EDGE_CURVE ( 'NONE', #75249, #32200, #37871, .T. ) ;
#51419=CARTESIAN_POINT ( 'NONE',  ( 16.49999999999990052, 19.08746187583904685, 4.000000000000000000 ) ) ;
#51420=EDGE_LOOP ( 'NONE', ( #70821, #46222, #11050, #49905 ) ) ;
#51421=ADVANCED_FACE ( 'NONE', ( #48033 ), #59629, .F. ) ;
#51422=LINE ( 'NONE', #116658, #11992 ) ;
#51423=CARTESIAN_POINT ( 'NONE',  ( 3.489213562373097322, -27.52281430457057709, 5.000000000000000000 ) ) ;
#51424=VECTOR ( 'NONE', #3298, 1000.000000000000000 ) ;
#51427=VERTEX_POINT ( 'NONE', #104520 ) ;
#51429=LINE ( 'NONE', #85444, #53592 ) ;
#51430=ORIENTED_EDGE ( 'NONE', *, *, #12104, .T. ) ;
#51431=CARTESIAN_POINT ( 'NONE',  ( -34.49999999999976552, 7.464255608400418573, 4.994342998332163219 ) ) ;
#51433=VECTOR ( 'NONE', #138939, 999.9999999999998863 ) ;
#51435=ORIENTED_EDGE ( 'NONE', *, *, #103716, .T. ) ;
#51436=VERTEX_POINT ( 'NONE', #3745 ) ;
#51437=VERTEX_POINT ( 'NONE', #135740 ) ;
#51438=DIRECTION ( 'NONE',  ( -0.000000000000000000, -0.3543493200069152693, 0.9351131265310292928 ) ) ;
#51439=PLANE ( 'NONE',  #142572 ) ;
#51441=VECTOR ( 'NONE', #138666, 1000.000000000000000 ) ;
#51442=DIRECTION ( 'NONE',  ( -0.000000000000000000, -0.3543493200069152693, 0.9351131265310292928 ) ) ;
#51445=ADVANCED_FACE ( 'NONE', ( #5177 ), #17508, .F. ) ;
#51446=VERTEX_POINT ( 'NONE', #82105 ) ;
#51447=( BOUNDED_CURVE ( )  B_SPLINE_CURVE ( 3, ( #44734, #67155, #56324, #24353 ),
 .UNSPECIFIED., .F., .T. ) 
 B_SPLINE_CURVE_WITH_KNOTS ( ( 4, 4 ),
 ( 5.143245962375972091, 6.645403452391246191 ),
 .UNSPECIFIED. ) 
 CURVE ( )  GEOMETRIC_REPRESENTATION_ITEM ( )  RATIONAL_B_SPLINE_CURVE ( ( 1.000000000000000000, 0.8206354192515258328, 0.8206354192515258328, 1.000000000000000000 ) ) 
 REPRESENTATION_ITEM ( '' )  );
#51448=ORIENTED_EDGE ( 'NONE', *, *, #69542, .T. ) ;
#51449=DIRECTION ( 'NONE',  ( 0.6830127018922181881, 0.6830127018922202975, -0.2588190451025214056 ) ) ;
#51450=EDGE_LOOP ( 'NONE', ( #69749, #98118, #138519, #8363 ) ) ;
#51451=VERTEX_POINT ( 'NONE', #50162 ) ;
#51452=AXIS2_PLACEMENT_3D ( 'NONE', #14497, #68908, #114511 ) ;
#51453=VECTOR ( 'NONE', #105020, 1000.000000000000000 ) ;
#51455=DIRECTION ( 'NONE',  ( 0.6830127018922181881, 0.6830127018922202975, -0.2588190451025214056 ) ) ;
#51456=VERTEX_POINT ( 'NONE', #126283 ) ;
#51457=VECTOR ( 'NONE', #11539, 1000.000000000000000 ) ;
#51458=LINE ( 'NONE', #95649, #50668 ) ;
#51460=ORIENTED_EDGE ( 'NONE', *, *, #120067, .T. ) ;
#51461=CARTESIAN_POINT ( 'NONE',  ( 10.88982677111781783, -22.22500000000000142, 4.785647885939352086 ) ) ;
#51462=CARTESIAN_POINT ( 'NONE',  ( -48.18398860626899705, 28.73617430169820608, 5.000000000000000000 ) ) ;
#51465=CARTESIAN_POINT ( 'NONE',  ( -4.499999999999968914, -2.568876922607790103, 4.000000000000000000 ) ) ;
#51466=LINE ( 'NONE', #142057, #42288 ) ;
#51467=ORIENTED_EDGE ( 'NONE', *, *, #43353, .T. ) ;
#51468=DIRECTION ( 'NONE',  ( -0.7071067811865486830, -0.7071067811865464625, -0.000000000000000000 ) ) ;
#51469=ORIENTED_EDGE ( 'NONE', *, *, #140543, .T. ) ;
#51470=VERTEX_POINT ( 'NONE', #103106 ) ;
#51471=VECTOR ( 'NONE', #703, 1000.000000000000114 ) ;
#51472=( BOUNDED_CURVE ( )  B_SPLINE_CURVE ( 3, ( #26926, #15305, #71176, #137856 ),
 .UNSPECIFIED., .F., .T. ) 
 B_SPLINE_CURVE_WITH_KNOTS ( ( 4, 4 ),
 ( 5.920967161967926273, 7.341195215986641820 ),
 .UNSPECIFIED. ) 
 CURVE ( )  GEOMETRIC_REPRESENTATION_ITEM ( )  RATIONAL_B_SPLINE_CURVE ( ( 1.000000000000000000, 0.8388583629366603844, 0.8388583629366603844, 1.000000000000000000 ) ) 
 REPRESENTATION_ITEM ( '' )  );
#51473=EDGE_LOOP ( 'NONE', ( #126004, #20895, #34025, #32392 ) ) ;
#51475=PLANE ( 'NONE',  #46496 ) ;
#51476=LINE ( 'NONE', #84804, #35740 ) ;
#51477=CARTESIAN_POINT ( 'NONE',  ( -34.49999999999976552, -2.945670655169033481, 4.994342998332163219 ) ) ;
#51478=CARTESIAN_POINT ( 'NONE',  ( 22.49999999999985434, 16.46639925780209524, 5.000000000000000000 ) ) ;
#51479=CARTESIAN_POINT ( 'NONE',  ( -1.499999999999984013, 7.087461875839178305, 4.000000000000000000 ) ) ;
#51480=LINE ( 'NONE', #63792, #133814 ) ;
#51481=VECTOR ( 'NONE', #44055, 1000.000000000000000 ) ;
#51483=VECTOR ( 'NONE', #36113, 1000.000000000000000 ) ;
#51484=LINE ( 'NONE', #29007, #116389 ) ;
#51487=CARTESIAN_POINT ( 'NONE',  ( -0.005480084712502889671, 28.92564299267938210, 4.000000000000000000 ) ) ;
#51488=CARTESIAN_POINT ( 'NONE',  ( 3.005480084712505828, 28.92564299267936079, 4.000000000000000000 ) ) ;
#51489=VERTEX_POINT ( 'NONE', #26961 ) ;
#51490=ORIENTED_EDGE ( 'NONE', *, *, #132645, .F. ) ;
#51491=ORIENTED_EDGE ( 'NONE', *, *, #120816, .T. ) ;
#51492=VECTOR ( 'NONE', #115511, 1000.000000000000000 ) ;
#51493=EDGE_LOOP ( 'NONE', ( #124344, #34051, #81648, #21631 ) ) ;
#51495=DIRECTION ( 'NONE',  ( -0.7071067811865486830, 0.7071067811865464625, 0.000000000000000000 ) ) ;
#51496=ORIENTED_EDGE ( 'NONE', *, *, #106, .F. ) ;
#51497=ADVANCED_FACE ( 'NONE', ( #71934 ), #91525, .F. ) ;
#51498=EDGE_LOOP ( 'NONE', ( #85606, #134980, #37129, #32089 ) ) ;
#51499=DIRECTION ( 'NONE',  ( -0.000000000000000000, 0.000000000000000000, 1.000000000000000000 ) ) ;
#51501=PLANE ( 'NONE',  #40993 ) ;
#51502=EDGE_CURVE ( 'NONE', #39673, #42516, #74046, .T. ) ;
#51504=CARTESIAN_POINT ( 'NONE',  ( 5.816011393731002066, 28.73617430169783304, 5.000000000000000000 ) ) ;
#51505=ORIENTED_EDGE ( 'NONE', *, *, #55197, .F. ) ;
#51506=FACE_OUTER_BOUND ( 'NONE', #104118, .T. ) ;
#51508=CARTESIAN_POINT ( 'NONE',  ( 28.49999999999981526, 22.08746187583901843, 4.000000000000000000 ) ) ;
#51509=EDGE_CURVE ( 'NONE', #121, #126591, #85610, .T. ) ;
#51510=EDGE_CURVE ( 'NONE', #3281, #130856, #86362, .T. ) ;
#51511=CARTESIAN_POINT ( 'NONE',  ( -22.49999999999984723, -6.839392718269148297, -8.480912228396030983 ) ) ;
#51513=ORIENTED_EDGE ( 'NONE', *, *, #137074, .F. ) ;
#51515=ADVANCED_FACE ( 'NONE', ( #87062 ), #108768, .F. ) ;
#51516=CARTESIAN_POINT ( 'NONE',  ( 15.70710678118643422, -9.740707523384182664, 5.000000000000000000 ) ) ;
#51518=ORIENTED_EDGE ( 'NONE', *, *, #133450, .F. ) ;
#51519=ORIENTED_EDGE ( 'NONE', *, *, #79405, .T. ) ;
#51521=ORIENTED_EDGE ( 'NONE', *, *, #39237, .T. ) ;
#51523=FACE_OUTER_BOUND ( 'NONE', #44010, .T. ) ;
#51524=LINE ( 'NONE', #86293, #79826 ) ;
#51525=LINE ( 'NONE', #31196, #24091 ) ;
#51526=ORIENTED_EDGE ( 'NONE', *, *, #65697, .T. ) ;
#51528=DIRECTION ( 'NONE',  ( -0.7071067811865487940, 0.7071067811865463515, -0.000000000000000000 ) ) ;
#51530=VECTOR ( 'NONE', #80233, 1000.000000000000000 ) ;
#51531=CARTESIAN_POINT ( 'NONE',  ( 5.994519915287488843, 28.92564299267942118, 4.000000000000000000 ) ) ;
#51532=CARTESIAN_POINT ( 'NONE',  ( 31.49999999999978684, -1.592773361805341459, -6.492772025301299266 ) ) ;
#51533=EDGE_LOOP ( 'NONE', ( #18024, #50904, #80591, #131217 ) ) ;
#51536=AXIS2_PLACEMENT_3D ( 'NONE', #54983, #55698, #68037 ) ;
#51538=CARTESIAN_POINT ( 'NONE',  ( 20.99999999999986855, 14.58746187583909482, 4.000000000000000000 ) ) ;
#51539=ORIENTED_EDGE ( 'NONE', *, *, #101494, .T. ) ;
#51540=FACE_OUTER_BOUND ( 'NONE', #49212, .T. ) ;
#51541=ORIENTED_EDGE ( 'NONE', *, *, #93045, .T. ) ;
#51542=LINE ( 'NONE', #95737, #111872 ) ;
#51543=CARTESIAN_POINT ( 'NONE',  ( 18.79289321881332953, 18.75929247661552779, 5.000000000000000000 ) ) ;
#51544=EDGE_CURVE ( 'NONE', #112859, #77801, #52280, .T. ) ;
#51545=EDGE_LOOP ( 'NONE', ( #78404, #12734, #133275, #81142 ) ) ;
#51546=CARTESIAN_POINT ( 'NONE',  ( -7.499999999999936939, -4.912538124160708897, 4.000000000000000000 ) ) ;
#51548=DIRECTION ( 'NONE',  ( -0.7071067811865486830, -0.7071067811865464625, 0.000000000000000000 ) ) ;
#51549=CARTESIAN_POINT ( 'NONE',  ( 21.18398860626899349, 28.73617430169802134, 5.000000000000000000 ) ) ;
#51552=AXIS2_PLACEMENT_3D ( 'NONE', #117030, #126467, #138810 ) ;
#51554=EDGE_CURVE ( 'NONE', #123479, #80179, #141442, .T. ) ;
#51555=DIRECTION ( 'NONE',  ( 0.6830127018922180770, -0.6830127018922204085, -0.2588190451025213501 ) ) ;
#51556=DIRECTION ( 'NONE',  ( -0.7071067811865487940, 0.7071067811865463515, -0.000000000000000000 ) ) ;
#51557=VECTOR ( 'NONE', #97547, 1000.000000000000000 ) ;
#51558=CARTESIAN_POINT ( 'NONE',  ( -38.75830541574789123, 0.7592924766157104211, 14.37146558664991680 ) ) ;
#51559=CARTESIAN_POINT ( 'NONE',  ( 0.000000000000000000, 0.000000000000000000, 5.000000000000000000 ) ) ;
#51560=LINE ( 'NONE', #19620, #124078 ) ;
#51561=ORIENTED_EDGE ( 'NONE', *, *, #40773, .T. ) ;
#51563=EDGE_LOOP ( 'NONE', ( #181, #92805, #12690, #50220 ) ) ;
#51567=ORIENTED_EDGE ( 'NONE', *, *, #96887, .T. ) ;
#51568=ADVANCED_FACE ( 'NONE', ( #140710 ), #131279, .F. ) ;
#51569=ORIENTED_EDGE ( 'NONE', *, *, #100955, .T. ) ;
#51570=DIRECTION ( 'NONE',  ( -0.6830127018922181881, 0.6830127018922202975, -0.2588190451025214056 ) ) ;
#51571=CARTESIAN_POINT ( 'NONE',  ( -36.48921356237310221, -27.52281430457080802, 5.000000000000000000 ) ) ;
#51572=AXIS2_PLACEMENT_3D ( 'NONE', #53381, #75174, #120771 ) ;
#51573=ORIENTED_EDGE ( 'NONE', *, *, #20117, .T. ) ;
#51574=CYLINDRICAL_SURFACE ( 'NONE', #16090, 0.5000000000000004441 ) ;
#51576=CARTESIAN_POINT ( 'NONE',  ( 39.18398860626899705, 28.73617430169814568, 5.000000000000000000 ) ) ;
#51577=LINE ( 'NONE', #39269, #32471 ) ;
#51580=EDGE_LOOP ( 'NONE', ( #142863, #3034, #58499, #100820 ) ) ;
#51581=DIRECTION ( 'NONE',  ( 0.7071067811865487940, 0.7071067811865463515, -0.000000000000000000 ) ) ;
#51582=DIRECTION ( 'NONE',  ( -0.6830127018922180770, -0.6830127018922204085, -0.2588190451025213501 ) ) ;
#51583=AXIS2_PLACEMENT_3D ( 'NONE', #110368, #22634, #34270 ) ;
#51584=FACE_OUTER_BOUND ( 'NONE', #143340, .T. ) ;
#51586=LINE ( 'NONE', #142861, #86192 ) ;
#51587=CARTESIAN_POINT ( 'NONE',  ( -3.489213562373097322, -27.52281430457057709, 5.000000000000000000 ) ) ;
#51589=ORIENTED_EDGE ( 'NONE', *, *, #103674, .T. ) ;
#51591=ORIENTED_EDGE ( 'NONE', *, *, #40735, .T. ) ;
#51592=ADVANCED_FACE ( 'NONE', ( #63896 ), #53738, .F. ) ;
#51593=DIRECTION ( 'NONE',  ( -0.7071067811865486830, 0.7071067811865464625, 0.000000000000000000 ) ) ;
#51594=DIRECTION ( 'NONE',  ( 0.7071067811865486830, -0.7071067811865464625, -0.000000000000000000 ) ) ;
#51597=DIRECTION ( 'NONE',  ( 1.000000000000000000, 0.000000000000000000, 0.000000000000000000 ) ) ;
#51599=VECTOR ( 'NONE', #85013, 1000.000000000000000 ) ;
#51600=CARTESIAN_POINT ( 'NONE',  ( 31.82816939922330945, 21.75929247661549581, 4.000000000000000000 ) ) ;
#51601=DIRECTION ( 'NONE',  ( -0.3543493200069162685, -0.000000000000000000, -0.9351131265310288487 ) ) ;
#51604=ORIENTED_EDGE ( 'NONE', *, *, #46492, .F. ) ;
#51605=PLANE ( 'NONE',  #73387 ) ;
#51606=ORIENTED_EDGE ( 'NONE', *, *, #23223, .F. ) ;
#51607=VECTOR ( 'NONE', #121361, 1000.000000000000000 ) ;
#51609=CARTESIAN_POINT ( 'NONE',  ( -8.186508646023558100, -15.74070752338411694, 8.904080028138961822 ) ) ;
#51611=CARTESIAN_POINT ( 'NONE',  ( 20.51078643762690490, -27.52281430457041012, 5.000000000000000000 ) ) ;
#51612=ORIENTED_EDGE ( 'NONE', *, *, #22525, .T. ) ;
#51616=LINE ( 'NONE', #82819, #21576 ) ;
#51618=CARTESIAN_POINT ( 'NONE',  ( 7.171830600776420539, -5.240707523384230626, 4.000000000000000000 ) ) ;
#51619=LINE ( 'NONE', #85637, #55435 ) ;
#51620=EDGE_CURVE ( 'NONE', #121270, #2749, #74785, .T. ) ;
#51621=AXIS2_PLACEMENT_3D ( 'NONE', #113375, #93073, #136559 ) ;
#51623=ORIENTED_EDGE ( 'NONE', *, *, #83427, .F. ) ;
#51624=CARTESIAN_POINT ( 'NONE',  ( -31.49999999999977973, -20.56887692260759337, 4.000000000000000000 ) ) ;
#51625=ORIENTED_EDGE ( 'NONE', *, *, #123833, .T. ) ;
#51626=VERTEX_POINT ( 'NONE', #40023 ) ;
#51628=EDGE_CURVE ( 'NONE', #115355, #101030, #95063, .T. ) ;
#51630=ADVANCED_FACE ( 'NONE', ( #29110 ), #62466, .T. ) ;
#51632=ORIENTED_EDGE ( 'NONE', *, *, #85034, .T. ) ;
#51633=VECTOR ( 'NONE', #29373, 1000.000000000000000 ) ;
#51635=VECTOR ( 'NONE', #96829, 1000.000000000000000 ) ;
#51636=PLANE ( 'NONE',  #16400 ) ;
#51637=FACE_BOUND ( 'NONE', #115341, .T. ) ;
#51638=ADVANCED_FACE ( 'NONE', ( #58591 ), #46263, .F. ) ;
#51639=CARTESIAN_POINT ( 'NONE',  ( -8.999999999999934275, -18.03360074219754949, 5.000000000000000000 ) ) ;
#51641=LINE ( 'NONE', #74836, #122591 ) ;
#51643=CARTESIAN_POINT ( 'NONE',  ( 42.48921356237308800, -27.52281430457085065, 5.000000000000000000 ) ) ;
#51644=ORIENTED_EDGE ( 'NONE', *, *, #64654, .F. ) ;
#51645=ORIENTED_EDGE ( 'NONE', *, *, #21907, .T. ) ;
#51646=CARTESIAN_POINT ( 'NONE',  ( -23.01844734635655954, 18.75929247661551713, 20.33588619593448144 ) ) ;
#51648=AXIS2_PLACEMENT_3D ( 'NONE', #26740, #118563, #70986 ) ;
#51650=VERTEX_POINT ( 'NONE', #13567 ) ;
#51651=DIRECTION ( 'NONE',  ( -0.7071067811865487940, 0.7071067811865463515, -0.000000000000000000 ) ) ;
#51652=DIRECTION ( 'NONE',  ( -0.7071067811865487940, 0.7071067811865463515, -0.000000000000000000 ) ) ;
#51653=AXIS2_PLACEMENT_3D ( 'NONE', #135771, #13247, #91555 ) ;
#51654=EDGE_LOOP ( 'NONE', ( #28916, #129345, #25548, #70765 ) ) ;
#51655=CARTESIAN_POINT ( 'NONE',  ( -11.51078643762690490, -27.52281430457047406, 5.000000000000000000 ) ) ;
#51656=VECTOR ( 'NONE', #4595, 1000.000000000000227 ) ;
#51657=DIRECTION ( 'NONE',  ( -0.000000000000000000, -0.3543493200069152693, 0.9351131265310292928 ) ) ;
#51658=DIRECTION ( 'NONE',  ( 0.3543493200069162685, -0.000000000000000000, -0.9351131265310288487 ) ) ;
#51659=FACE_OUTER_BOUND ( 'NONE', #88151, .T. ) ;
#51660=CARTESIAN_POINT ( 'NONE',  ( 12.48921356237309155, -27.52281430457064104, 5.000000000000000000 ) ) ;
#51661=LINE ( 'NONE', #8794, #115812 ) ;
#51662=ORIENTED_EDGE ( 'NONE', *, *, #68906, .T. ) ;
#51663=VECTOR ( 'NONE', #3023, 1000.000000000000000 ) ;
#51664=ORIENTED_EDGE ( 'NONE', *, *, #40276, .T. ) ;
#51666=CARTESIAN_POINT ( 'NONE',  ( -28.17183060077627488, -8.240707523384195099, 4.000000000000000000 ) ) ;
#51668=VERTEX_POINT ( 'NONE', #2703 ) ;
#51669=ORIENTED_EDGE ( 'NONE', *, *, #77504, .F. ) ;
#51670=CARTESIAN_POINT ( 'NONE',  ( 0.000000000000000000, 0.000000000000000000, 5.000000000000000000 ) ) ;
#51671=FACE_OUTER_BOUND ( 'NONE', #65178, .T. ) ;
#51672=EDGE_CURVE ( 'NONE', #132730, #110607, #80311, .T. ) ;
#51674=VECTOR ( 'NONE', #83145, 1000.000000000000227 ) ;
#51675=VERTEX_POINT ( 'NONE', #57847 ) ;
#51676=DIRECTION ( 'NONE',  ( 0.7071067811865487940, 0.7071067811865463515, -0.000000000000000000 ) ) ;
#51678=EDGE_CURVE ( 'NONE', #84275, #87748, #81013, .T. ) ;
#51679=EDGE_CURVE ( 'NONE', #49159, #48229, #48366, .T. ) ;
#51681=CARTESIAN_POINT ( 'NONE',  ( 59.99451991528749772, 28.92564299267980132, 4.000000000000000000 ) ) ;
#51682=ADVANCED_FACE ( 'NONE', ( #70172 ), #4081, .F. ) ;
#51683=VERTEX_POINT ( 'NONE', #142867 ) ;
#51685=EDGE_CURVE ( 'NONE', #49717, #39409, #114332, .T. ) ;
#51686=DIRECTION ( 'NONE',  ( 0.7071067811865486830, -0.7071067811865464625, -0.000000000000000000 ) ) ;
#51687=DIRECTION ( 'NONE',  ( 0.3543493200069162685, -0.000000000000000000, -0.9351131265310288487 ) ) ;
#51690=ORIENTED_EDGE ( 'NONE', *, *, #128910, .T. ) ;
#51692=EDGE_LOOP ( 'NONE', ( #82076, #92769, #3689, #90425 ) ) ;
#51693=EDGE_CURVE ( 'NONE', #75711, #49314, #59283, .T. ) ;
#51695=DIRECTION ( 'NONE',  ( 1.000000000000000000, 0.000000000000000000, 0.000000000000000000 ) ) ;
#51697=AXIS2_PLACEMENT_3D ( 'NONE', #45794, #132811, #47255 ) ;
#51698=EDGE_LOOP ( 'NONE', ( #80851, #107105, #46488, #138436 ) ) ;
#51699=ADVANCED_FACE ( 'NONE', ( #124497 ), #102037, .F. ) ;
#51700=CARTESIAN_POINT ( 'NONE',  ( 24.91272823266826109, 2.053671025133813277, 5.000000000000000000 ) ) ;
#51701=FACE_OUTER_BOUND ( 'NONE', #141494, .T. ) ;
#51702=DIRECTION ( 'NONE',  ( 0.000000000000000000, 0.000000000000000000, 1.000000000000000000 ) ) ;
#51703=VECTOR ( 'NONE', #116218, 1000.000000000000000 ) ;
#51704=ORIENTED_EDGE ( 'NONE', *, *, #80863, .F. ) ;
#51706=CARTESIAN_POINT ( 'NONE',  ( 0.000000000000000000, 0.000000000000000000, 5.000000000000000000 ) ) ;
#51707=LINE ( 'NONE', #7442, #125728 ) ;
#51709=CARTESIAN_POINT ( 'NONE',  ( 0.7123099396602788902, -21.73547319004781642, 4.999917730833664642 ) ) ;
#51710=ADVANCED_FACE ( 'NONE', ( #79629 ), #43554, .T. ) ;
#51711=CARTESIAN_POINT ( 'NONE',  ( -60.48921356237309510, -27.52281430457097500, 5.000000000000000000 ) ) ;
#51712=LINE ( 'NONE', #140147, #113206 ) ;
#51713=EDGE_LOOP ( 'NONE', ( #85174, #27069, #85669, #104297, #78756 ) ) ;
#51714=VERTEX_POINT ( 'NONE', #26614 ) ;
#51715=DIRECTION ( 'NONE',  ( 0.7071067811865487940, 0.7071067811865463515, 0.000000000000000000 ) ) ;
#51719=LINE ( 'NONE', #94475, #87545 ) ;
#51720=VECTOR ( 'NONE', #8004, 1000.000000000000000 ) ;
#51721=LINE ( 'NONE', #37996, #57643 ) ;
#51722=CARTESIAN_POINT ( 'NONE',  ( 14.99999999999990230, -1.447814304570822053, 5.000000000000000000 ) ) ;
#51723=ORIENTED_EDGE ( 'NONE', *, *, #81909, .T. ) ;
#51725=LINE ( 'NONE', #52408, #56304 ) ;
#51726=PLANE ( 'NONE',  #43689 ) ;
#51728=VECTOR ( 'NONE', #65621, 1000.000000000000000 ) ;
#51729=DIRECTION ( 'NONE',  ( 0.7071067811865486830, -0.7071067811865464625, -0.000000000000000000 ) ) ;
#51730=VERTEX_POINT ( 'NONE', #91859 ) ;
#51731=PLANE ( 'NONE',  #46522 ) ;
#51732=VECTOR ( 'NONE', #125440, 1000.000000000000000 ) ;
#51733=EDGE_LOOP ( 'NONE', ( #72268, #135276, #87572, #119602 ) ) ;
#51736=DIRECTION ( 'NONE',  ( 0.6830127018922180770, -0.6830127018922204085, -0.2588190451025213501 ) ) ;
#51737=DIRECTION ( 'NONE',  ( -0.7071067811865486830, -0.7071067811865464625, 0.000000000000000000 ) ) ;
#51738=( BOUNDED_CURVE ( )  B_SPLINE_CURVE ( 3, ( #36698, #48297, #37437, #115655 ),
 .UNSPECIFIED., .F., .F. ) 
 B_SPLINE_CURVE_WITH_KNOTS ( ( 4, 4 ),
 ( 1.901594255663617172, 1.933014472006534534 ),
 .UNSPECIFIED. ) 
 CURVE ( )  GEOMETRIC_REPRESENTATION_ITEM ( )  RATIONAL_B_SPLINE_CURVE ( ( 1.000000000000000000, 0.9999177325257868620, 0.9999177325257868620, 1.000000000000000000 ) ) 
 REPRESENTATION_ITEM ( '' )  );
#51739=EDGE_CURVE ( 'NONE', #63249, #44387, #139136, .T. ) ;
#51741=CARTESIAN_POINT ( 'NONE',  ( -4.499999999999962697, -17.94781430457065241, 5.000000000000000000 ) ) ;
#51742=VECTOR ( 'NONE', #43849, 1000.000000000000000 ) ;
#51743=LINE ( 'NONE', #110357, #44001 ) ;
#51744=LINE ( 'NONE', #21234, #71986 ) ;
#51745=CARTESIAN_POINT ( 'NONE',  ( 32.99451991528749062, 28.92564299267960948, 4.000000000000000000 ) ) ;
#51746=ORIENTED_EDGE ( 'NONE', *, *, #90683, .T. ) ;
#51747=DIRECTION ( 'NONE',  ( -0.3543493200069163240, -0.000000000000000000, 0.9351131265310288487 ) ) ;
#51748=LINE ( 'NONE', #17647, #42296 ) ;
#51749=CARTESIAN_POINT ( 'NONE',  ( 32.99999999999977973, -0.8619312979531654761, -5.102805207349749850 ) ) ;
#51750=CARTESIAN_POINT ( 'NONE',  ( 29.11162361894740513, 9.759292476615618384, 17.35367589129205967 ) ) ;
#51751=CARTESIAN_POINT ( 'NONE',  ( -6.489213562373093325, -27.52281430457059841, 5.000000000000000000 ) ) ;
#51752=EDGE_CURVE ( 'NONE', #23719, #132598, #66051, .T. ) ;
#51756=VECTOR ( 'NONE', #30102, 1000.000000000000227 ) ;
#51759=VERTEX_POINT ( 'NONE', #36085 ) ;
#51761=DIRECTION ( 'NONE',  ( 1.000000000000000000, 0.000000000000000000, 0.000000000000000000 ) ) ;
#51762=EDGE_CURVE ( 'NONE', #2559, #141411, #25172, .T. ) ;
#51763=LINE ( 'NONE', #85079, #2234 ) ;
#51765=ORIENTED_EDGE ( 'NONE', *, *, #130933, .F. ) ;
#51766=LINE ( 'NONE', #49645, #118529 ) ;
#51768=EDGE_LOOP ( 'NONE', ( #41881, #53685, #126149, #86836, #141197, #141337 ) ) ;
#51769=DIRECTION ( 'NONE',  ( -0.6830127018922180770, -0.6830127018922204085, -0.2588190451025213501 ) ) ;
#51770=ORIENTED_EDGE ( 'NONE', *, *, #116005, .F. ) ;
#51771=ORIENTED_EDGE ( 'NONE', *, *, #30027, .F. ) ;
#51773=CARTESIAN_POINT ( 'NONE',  ( 34.82816939922328459, -2.240707523384267930, 4.000000000000000000 ) ) ;
#51774=CARTESIAN_POINT ( 'NONE',  ( -29.99451991528749417, 28.92564299267958816, 4.000000000000000000 ) ) ;
#51777=VERTEX_POINT ( 'NONE', #3407 ) ;
#51779=CARTESIAN_POINT ( 'NONE',  ( -12.70701326429296252, -21.74070752338406010, 4.999753212805220670 ) ) ;
#51780=CARTESIAN_POINT ( 'NONE',  ( 13.22674160717825842, -11.24070752338416135, 18.24660765846985200 ) ) ;
#51781=LINE ( 'NONE', #105410, #82337 ) ;
#51782=ORIENTED_EDGE ( 'NONE', *, *, #33505, .T. ) ;
#51785=EDGE_CURVE ( 'NONE', #74639, #136354, #59971, .T. ) ;
#51788=CARTESIAN_POINT ( 'NONE',  ( 30.29974487139158867, -27.71228299555227537, 4.000000000000000000 ) ) ;
#51789=CARTESIAN_POINT ( 'NONE',  ( -29.29289321881324426, -18.74070752338408852, 5.000000000000000000 ) ) ;
#51790=DIRECTION ( 'NONE',  ( 0.7071067811865487940, 0.7071067811865463515, 0.000000000000000000 ) ) ;
#51791=ORIENTED_EDGE ( 'NONE', *, *, #102615, .F. ) ;
#51792=EDGE_CURVE ( 'NONE', #95280, #34098, #73689, .T. ) ;
#51793=EDGE_LOOP ( 'NONE', ( #78785, #10248, #125354, #113329 ) ) ;
#51794=AXIS2_PLACEMENT_3D ( 'NONE', #81087, #35461, #100691 ) ;
#51795=CARTESIAN_POINT ( 'NONE',  ( 0.000000000000000000, 0.000000000000000000, 5.000000000000000000 ) ) ;
#51797=CARTESIAN_POINT ( 'NONE',  ( -8.816011393731004731, 28.73617430169781173, 5.000000000000000000 ) ) ;
#51798=CARTESIAN_POINT ( 'NONE',  ( -51.18398860626899705, 28.73617430169823095, 5.000000000000000000 ) ) ;
#51799=ORIENTED_EDGE ( 'NONE', *, *, #138459, .T. ) ;
#51800=EDGE_LOOP ( 'NONE', ( #25400, #51047, #121685, #98069 ) ) ;
#51801=CARTESIAN_POINT ( 'NONE',  ( -14.99999999999988809, 14.96639925780210412, 5.000000000000000000 ) ) ;
#51803=ORIENTED_EDGE ( 'NONE', *, *, #60849, .F. ) ;
#51805=EDGE_CURVE ( 'NONE', #133751, #3412, #129480, .T. ) ;
#51806=ORIENTED_EDGE ( 'NONE', *, *, #129461, .T. ) ;
#51807=EDGE_CURVE ( 'NONE', #69645, #20118, #51239, .T. ) ;
#51808=CARTESIAN_POINT ( 'NONE',  ( -42.18398860626899705, 28.73617430169816700, 5.000000000000000000 ) ) ;
#51809=EDGE_LOOP ( 'NONE', ( #138296, #83843, #35646, #59223 ) ) ;
#51810=DIRECTION ( 'NONE',  ( -0.000000000000000000, 0.3543493200069153248, 0.9351131265310291818 ) ) ;
#51811=ADVANCED_FACE ( 'NONE', ( #9686 ), #8239, .F. ) ;
#51813=FACE_BOUND ( 'NONE', #90176, .T. ) ;
#51814=EDGE_CURVE ( 'NONE', #14957, #38790, #49826, .T. ) ;
#51815=CARTESIAN_POINT ( 'NONE',  ( -34.75611968250420603, -4.294349301475885561, 4.955485411084901592 ) ) ;
#51816=CARTESIAN_POINT ( 'NONE',  ( 33.18398860626899705, 28.73617430169810305, 5.000000000000000000 ) ) ;
#51817=ORIENTED_EDGE ( 'NONE', *, *, #21388, .F. ) ;
#51821=ORIENTED_EDGE ( 'NONE', *, *, #115101, .F. ) ;
#51822=AXIS2_PLACEMENT_3D ( 'NONE', #57279, #136223, #68864 ) ;
#51823=ORIENTED_EDGE ( 'NONE', *, *, #9039, .F. ) ;
#51825=VERTEX_POINT ( 'NONE', #38920 ) ;
#51826=PLANE ( 'NONE',  #61597 ) ;
#51827=FACE_OUTER_BOUND ( 'NONE', #98779, .T. ) ;
#51828=DIRECTION ( 'NONE',  ( 0.7071067811865487940, 0.7071067811865463515, 0.000000000000000000 ) ) ;
#51829=VECTOR ( 'NONE', #80755, 1000.000000000000000 ) ;
#51830=DIRECTION ( 'NONE',  ( -0.000000000000000000, -0.000000000000000000, 1.000000000000000000 ) ) ;
#51831=DIRECTION ( 'NONE',  ( -0.000000000000000000, 0.000000000000000000, 1.000000000000000000 ) ) ;
#51832=CARTESIAN_POINT ( 'NONE',  ( 3.005480084712505828, 28.92564299267936079, 4.000000000000000000 ) ) ;
#51834=DIRECTION ( 'NONE',  ( -0.7071067811865486830, -0.7071067811865464625, 0.000000000000000000 ) ) ;
#51835=CARTESIAN_POINT ( 'NONE',  ( 21.48921356237309155, -27.52281430457070499, 5.000000000000000000 ) ) ;
#51837=PLANE ( 'NONE',  #130274 ) ;
#51838=ORIENTED_EDGE ( 'NONE', *, *, #11688, .F. ) ;
#51839=CARTESIAN_POINT ( 'NONE',  ( -3.183988606268992161, 28.73617430169789699, 5.000000000000000000 ) ) ;
#51840=CARTESIAN_POINT ( 'NONE',  ( -27.69326993309582008, -3.740707523384241728, 12.88036043432873967 ) ) ;
#51842=EDGE_LOOP ( 'NONE', ( #24447, #31586, #89923, #29660 ) ) ;
#51843=AXIS2_PLACEMENT_3D ( 'NONE', #26889, #71135, #86289 ) ;
#51844=ORIENTED_EDGE ( 'NONE', *, *, #14016, .T. ) ;
#51846=VERTEX_POINT ( 'NONE', #104883 ) ;
#51847=VECTOR ( 'NONE', #28727, 1000.000000000000000 ) ;
#51848=PLANE ( 'NONE',  #53305 ) ;
#51849=VECTOR ( 'NONE', #111547, 999.9999999999998863 ) ;
#51850=ADVANCED_FACE ( 'NONE', ( #83143 ), #28771, .F. ) ;
#51851=VECTOR ( 'NONE', #14569, 1000.000000000000000 ) ;
#51855=EDGE_CURVE ( 'NONE', #45746, #107805, #71560, .T. ) ;
#51856=EDGE_LOOP ( 'NONE', ( #16586, #89380, #143439, #72406 ) ) ;
#51858=DIRECTION ( 'NONE',  ( 0.3543493200069162685, -0.000000000000000000, -0.9351131265310288487 ) ) ;
#51859=EDGE_CURVE ( 'NONE', #94800, #63599, #4802, .T. ) ;
#51860=ORIENTED_EDGE ( 'NONE', *, *, #53136, .F. ) ;
#51861=DIRECTION ( 'NONE',  ( 1.000000000000000000, 0.000000000000000000, 0.000000000000000000 ) ) ;
#51862=VECTOR ( 'NONE', #62084, 1000.000000000000227 ) ;
#51863=DIRECTION ( 'NONE',  ( 0.000000000000000000, 0.000000000000000000, 1.000000000000000000 ) ) ;
#51864=DIRECTION ( 'NONE',  ( 0.6830127018922181881, 0.6830127018922202975, -0.2588190451025214056 ) ) ;
#51865=VERTEX_POINT ( 'NONE', #15686 ) ;
#51866=ORIENTED_EDGE ( 'NONE', *, *, #115191, .T. ) ;
#51867=EDGE_CURVE ( 'NONE', #71156, #113103, #138962, .T. ) ;
#51869=ORIENTED_EDGE ( 'NONE', *, *, #140266, .F. ) ;
#51871=ORIENTED_EDGE ( 'NONE', *, *, #75588, .F. ) ;
#51872=ORIENTED_EDGE ( 'NONE', *, *, #37156, .T. ) ;
#51874=EDGE_CURVE ( 'NONE', #50240, #108415, #60716, .T. ) ;
#51875=CARTESIAN_POINT ( 'NONE',  ( 30.18398860626900060, 28.73617430169808173, 5.000000000000000000 ) ) ;
#51876=VECTOR ( 'NONE', #90569, 1000.000000000000000 ) ;
#51877=FACE_OUTER_BOUND ( 'NONE', #61438, .T. ) ;
#51878=DIRECTION ( 'NONE',  ( -0.7071067811865487940, 0.7071067811865463515, 0.000000000000000000 ) ) ;
#51879=ADVANCED_FACE ( 'NONE', ( #105574 ), #6235, .F. ) ;
#51880=CARTESIAN_POINT ( 'NONE',  ( -2.671830600776447184, 14.25929247661557397, 4.000000000000000000 ) ) ;
#51881=DIRECTION ( 'NONE',  ( -0.7071067811865487940, 0.7071067811865463515, -0.000000000000000000 ) ) ;
#51882=EDGE_CURVE ( 'NONE', #133731, #124530, #117168, .T. ) ;
#51883=ORIENTED_EDGE ( 'NONE', *, *, #99478, .F. ) ;
#51884=DIRECTION ( 'NONE',  ( -0.000000000000000000, 0.3543493200069153248, 0.9351131265310292928 ) ) ;
#51885=VERTEX_POINT ( 'NONE', #383 ) ;
#51886=CARTESIAN_POINT ( 'NONE',  ( 23.99999999999983302, 13.93112307739204425, 4.000000000000000000 ) ) ;
#51887=ADVANCED_FACE ( 'NONE', ( #75149 ), #109880, .F. ) ;
#51889=PLANE ( 'NONE',  #124955 ) ;
#51890=AXIS2_PLACEMENT_3D ( 'NONE', #91956, #123902, #14405 ) ;
#51891=EDGE_LOOP ( 'NONE', ( #99755, #32320, #36205, #95859 ) ) ;
#51892=CARTESIAN_POINT ( 'NONE',  ( -29.29289321881324426, -9.740707523384182664, 5.000000000000000000 ) ) ;
#51893=ORIENTED_EDGE ( 'NONE', *, *, #95529, .F. ) ;
#51894=VERTEX_POINT ( 'NONE', #21454 ) ;
#51896=FACE_OUTER_BOUND ( 'NONE', #53848, .T. ) ;
#51897=CARTESIAN_POINT ( 'NONE',  ( -26.99451991528749417, 28.92564299267956685, 4.000000000000000000 ) ) ;
#51898=CARTESIAN_POINT ( 'NONE',  ( -30.48921356237309510, -27.52281430457076894, 5.000000000000000000 ) ) ;
#51899=CARTESIAN_POINT ( 'NONE',  ( 69.48921356237309510, -27.52281430457103895, 5.000000000000000000 ) ) ;
#51902=CARTESIAN_POINT ( 'NONE',  ( -5.671830600776424092, -12.74070752338414891, 4.000000000000000000 ) ) ;
#51903=CARTESIAN_POINT ( 'NONE',  ( 57.48921356237308800, -27.52281430457095368, 5.000000000000000000 ) ) ;
#51904=DIRECTION ( 'NONE',  ( 0.7071067811865487940, 0.7071067811865463515, -0.000000000000000000 ) ) ;
#51905=DIRECTION ( 'NONE',  ( -0.7071067811865486830, 0.7071067811865464625, 0.000000000000000000 ) ) ;
#51907=DIRECTION ( 'NONE',  ( 1.000000000000000000, 0.000000000000000000, 0.000000000000000000 ) ) ;
#51908=EDGE_CURVE ( 'NONE', #26241, #132436, #76569, .T. ) ;
#51909=ORIENTED_EDGE ( 'NONE', *, *, #89786, .F. ) ;
#51910=CARTESIAN_POINT ( 'NONE',  ( -10.82334089840020930, 5.259292476615665457, 15.86257073897100511 ) ) ;
#51911=LINE ( 'NONE', #30127, #36031 ) ;
#51912=ORIENTED_EDGE ( 'NONE', *, *, #129229, .F. ) ;
#51913=CARTESIAN_POINT ( 'NONE',  ( -8.999999999999937828, -5.527737879153202805, -7.983877177622351162 ) ) ;
#51914=LINE ( 'NONE', #39619, #30265 ) ;
#51915=ORIENTED_EDGE ( 'NONE', *, *, #70876, .F. ) ;
#51916=DIRECTION ( 'NONE',  ( -0.7071067811865486830, -0.7071067811865464625, 0.000000000000000000 ) ) ;
#51917=DIRECTION ( 'NONE',  ( 0.3543493200069162685, -0.000000000000000000, -0.9351131265310288487 ) ) ;
#51918=ORIENTED_EDGE ( 'NONE', *, *, #95529, .T. ) ;
#51919=EDGE_LOOP ( 'NONE', ( #17478, #99688, #92565 ) ) ;
#51920=PLANE ( 'NONE',  #6972 ) ;
#51921=LINE ( 'NONE', #86692, #88448 ) ;
#51922=AXIS2_PLACEMENT_3D ( 'NONE', #38111, #138849, #127225 ) ;
#51923=CARTESIAN_POINT ( 'NONE',  ( -33.75860074219772855, 21.72500000000000142, 5.000000000000000000 ) ) ;
#51924=EDGE_CURVE ( 'NONE', #139982, #16938, #65717, .T. ) ;
#51927=AXIS2_PLACEMENT_3D ( 'NONE', #14983, #61920, #80284 ) ;
#51928=FACE_OUTER_BOUND ( 'NONE', #53569, .T. ) ;
#51929=ORIENTED_EDGE ( 'NONE', *, *, #137788, .F. ) ;
#51930=CARTESIAN_POINT ( 'NONE',  ( -20.99451991528748707, 28.92564299267952777, 4.000000000000000000 ) ) ;
#51931=ADVANCED_FACE ( 'NONE', ( #20718 ), #22139, .F. ) ;
#51934=CARTESIAN_POINT ( 'NONE',  ( 14.67183060077636725, -12.74070752338415069, 4.000000000000000000 ) ) ;
#51935=ORIENTED_EDGE ( 'NONE', *, *, #38303, .T. ) ;
#51936=DIRECTION ( 'NONE',  ( -0.7071067811865487940, 0.7071067811865463515, 0.000000000000000000 ) ) ;
#51937=ORIENTED_EDGE ( 'NONE', *, *, #405, .T. ) ;
#51938=AXIS2_PLACEMENT_3D ( 'NONE', #3512, #47804, #82540 ) ;
#51939=ADVANCED_FACE ( 'NONE', ( #31618 ), #64245, .F. ) ;
#51941=CARTESIAN_POINT ( 'NONE',  ( 6.183988606268994381, 28.73617430169791476, 5.000000000000000000 ) ) ;
#51943=VERTEX_POINT ( 'NONE', #142531 ) ;
#51944=CARTESIAN_POINT ( 'NONE',  ( -4.499999999999972466, 21.05218569542895679, 5.000000000000000000 ) ) ;
#51945=DIRECTION ( 'NONE',  ( -0.6830127018922181881, 0.6830127018922202975, -0.2588190451025214056 ) ) ;
#51946=VECTOR ( 'NONE', #87867, 1000.000000000000000 ) ;
#51948=EDGE_CURVE ( 'NONE', #83415, #92406, #64976, .T. ) ;
#51949=LINE ( 'NONE', #118607, #77591 ) ;
#51950=VERTEX_POINT ( 'NONE', #88870 ) ;
#51951=CARTESIAN_POINT ( 'NONE',  ( -39.18398860626899705, 28.73617430169814568, 5.000000000000000000 ) ) ;
#51954=CARTESIAN_POINT ( 'NONE',  ( -38.99451991528749062, 28.92564299267965211, 4.000000000000000000 ) ) ;
#51955=AXIS2_PLACEMENT_3D ( 'NONE', #19570, #108684, #42782 ) ;
#51956=EDGE_LOOP ( 'NONE', ( #31503, #66467, #2812, #108028 ) ) ;
#51960=ORIENTED_EDGE ( 'NONE', *, *, #26831, .F. ) ;
#51961=DIRECTION ( 'NONE',  ( 0.3543493200069162685, -0.000000000000000000, -0.9351131265310288487 ) ) ;
#51962=CARTESIAN_POINT ( 'NONE',  ( -19.00193056682084247, -22.22500000000000142, 4.500000000000000888 ) ) ;
#51963=DIRECTION ( 'NONE',  ( 0.7071067811865487940, -0.7071067811865463515, 0.000000000000000000 ) ) ;
#51964=DIRECTION ( 'NONE',  ( -0.7071067811865486830, -0.7071067811865464625, -0.000000000000000000 ) ) ;
#51965=ORIENTED_EDGE ( 'NONE', *, *, #99024, .F. ) ;
#51966=LINE ( 'NONE', #19323, #76931 ) ;
#51968=VERTEX_POINT ( 'NONE', #43218 ) ;
#51970=CARTESIAN_POINT ( 'NONE',  ( 19.49999999999985789, 1.030536316426522436, -5.498701923753846366 ) ) ;
#51971=LINE ( 'NONE', #96149, #140492 ) ;
#51972=CARTESIAN_POINT ( 'NONE',  ( 0.000000000000000000, 0.000000000000000000, 5.000000000000000000 ) ) ;
#51973=ORIENTED_EDGE ( 'NONE', *, *, #122041, .T. ) ;
#51975=ADVANCED_FACE ( 'NONE', ( #131650 ), #13396, .F. ) ;
#51976=DIRECTION ( 'NONE',  ( 0.7071067811865487940, 0.7071067811865463515, -0.000000000000000000 ) ) ;
#51977=ADVANCED_FACE ( 'NONE', ( #56964 ), #134508, .F. ) ;
#51978=DIRECTION ( 'NONE',  ( 0.7071067811865487940, 0.7071067811865463515, 0.000000000000000000 ) ) ;
#51979=FACE_OUTER_BOUND ( 'NONE', #70063, .T. ) ;
#51981=CARTESIAN_POINT ( 'NONE',  ( -7.499999999999951150, -2.173586137069146051, -4.605770156576128649 ) ) ;
#51982=CARTESIAN_POINT ( 'NONE',  ( -2.331532588401415307, -18.74070752338408496, 20.73178291233840298 ) ) ;
#51984=ORIENTED_EDGE ( 'NONE', *, *, #52461, .F. ) ;
#51985=ORIENTED_EDGE ( 'NONE', *, *, #10218, .T. ) ;
#51986=EDGE_LOOP ( 'NONE', ( #34396, #116685, #17169, #82761 ) ) ;
#51987=ORIENTED_EDGE ( 'NONE', *, *, #71017, .F. ) ;
#51988=CARTESIAN_POINT ( 'NONE',  ( -18.29974487139159223, -27.71228299555219010, 4.000000000000000000 ) ) ;
#51989=EDGE_CURVE ( 'NONE', #142104, #44292, #2517, .T. ) ;
#51990=VECTOR ( 'NONE', #115980, 1000.000000000000000 ) ;
#51991=CARTESIAN_POINT ( 'NONE',  ( 5.510786437626906675, -27.52281430457051314, 5.000000000000000000 ) ) ;
#51992=VERTEX_POINT ( 'NONE', #124325 ) ;
#51993=CARTESIAN_POINT ( 'NONE',  ( -24.48921356237309510, -27.52281430457072631, 5.000000000000000000 ) ) ;
#51994=DIRECTION ( 'NONE',  ( 0.7071067811865486830, -0.7071067811865464625, -0.000000000000000000 ) ) ;
#51995=CARTESIAN_POINT ( 'NONE',  ( 2.207106781186526590, -20.24070752338407431, 5.000000000000000000 ) ) ;
#51996=LINE ( 'NONE', #60772, #18338 ) ;
#51998=ORIENTED_EDGE ( 'NONE', *, *, #68123, .F. ) ;
#51999=DIRECTION ( 'NONE',  ( -0.3543493200069162685, -0.000000000000000000, -0.9351131265310288487 ) ) ;
#52001=EDGE_LOOP ( 'NONE', ( #77540, #15027, #77920, #123333 ) ) ;
#52002=CARTESIAN_POINT ( 'NONE',  ( -27.18398860626900060, 28.73617430169806042, 5.000000000000000000 ) ) ;
#52003=ORIENTED_EDGE ( 'NONE', *, *, #27940, .F. ) ;
#52004=CARTESIAN_POINT ( 'NONE',  ( 24.48921356237309510, -27.52281430457072631, 5.000000000000000000 ) ) ;
#52005=VERTEX_POINT ( 'NONE', #3244 ) ;
#52008=ORIENTED_EDGE ( 'NONE', *, *, #72900, .T. ) ;
#52009=EDGE_LOOP ( 'NONE', ( #103572, #125944, #108718, #61592 ) ) ;
#52010=LINE ( 'NONE', #96194, #129860 ) ;
#52011=VECTOR ( 'NONE', #124837, 1000.000000000000000 ) ;
#52013=DIRECTION ( 'NONE',  ( -0.000000000000000000, 0.3543493200069153248, 0.9351131265310292928 ) ) ;
#52015=CARTESIAN_POINT ( 'NONE',  ( -6.489213562373093325, -27.52281430457059841, 5.000000000000000000 ) ) ;
#52016=EDGE_CURVE ( 'NONE', #62936, #80963, #123647, .T. ) ;
#52017=AXIS2_PLACEMENT_3D ( 'NONE', #75637, #9628, #21243 ) ;
#52018=CARTESIAN_POINT ( 'NONE',  ( 74.99451991528749772, 28.92564299267990435, 4.000000000000000000 ) ) ;
#52019=DIRECTION ( 'NONE',  ( 0.7071067811865486830, -0.7071067811865464625, -0.000000000000000000 ) ) ;
#52020=FACE_OUTER_BOUND ( 'NONE', #40710, .T. ) ;
#52022=EDGE_CURVE ( 'NONE', #135619, #10069, #80144, .T. ) ;
#52023=CARTESIAN_POINT ( 'NONE',  ( 14.99999999999990941, 11.58746187583913034, 4.000000000000000000 ) ) ;
#52026=CARTESIAN_POINT ( 'NONE',  ( -34.49999999999975131, 11.52377502935399889, -1.522421517564005899 ) ) ;
#52027=VECTOR ( 'NONE', #125887, 999.9999999999998863 ) ;
#52028=ORIENTED_EDGE ( 'NONE', *, *, #19235, .T. ) ;
#52029=ORIENTED_EDGE ( 'NONE', *, *, #44575, .F. ) ;
#52030=ORIENTED_EDGE ( 'NONE', *, *, #134532, .T. ) ;
#52031=ORIENTED_EDGE ( 'NONE', *, *, #82155, .F. ) ;
#52033=CARTESIAN_POINT ( 'NONE',  ( -20.67183060077632817, -15.74070752338412404, 4.000000000000000000 ) ) ;
#52035=PLANE ( 'NONE',  #13887 ) ;
#52036=ADVANCED_FACE ( 'NONE', ( #91694 ), #91013, .F. ) ;
#52037=ORIENTED_EDGE ( 'NONE', *, *, #35581, .T. ) ;
#52039=VERTEX_POINT ( 'NONE', #100443 ) ;
#52040=ADVANCED_FACE ( 'NONE', ( #14842 ), #35924, .F. ) ;
#52042=AXIS2_PLACEMENT_3D ( 'NONE', #93589, #115285, #60267 ) ;
#52044=LINE ( 'NONE', #26713, #79477 ) ;
#52045=DIRECTION ( 'NONE',  ( -0.7071067811865486830, -0.7071067811865464625, -0.000000000000000000 ) ) ;
#52046=VECTOR ( 'NONE', #136842, 1000.000000000000000 ) ;
#52047=CARTESIAN_POINT ( 'NONE',  ( -33.18398860626899705, 28.73617430169810305, 5.000000000000000000 ) ) ;
#52048=ORIENTED_EDGE ( 'NONE', *, *, #73753, .F. ) ;
#52049=ORIENTED_EDGE ( 'NONE', *, *, #52798, .F. ) ;
#52050=EDGE_LOOP ( 'NONE', ( #53443, #142866, #58961, #39757 ) ) ;
#52053=ADVANCED_FACE ( 'NONE', ( #25722 ), #114160, .F. ) ;
#52054=LINE ( 'NONE', #51346, #12602 ) ;
#52055=DIRECTION ( 'NONE',  ( -0.7071067811865487940, 0.7071067811865463515, 0.000000000000000000 ) ) ;
#52056=DIRECTION ( 'NONE',  ( -0.6830127018922181881, 0.6830127018922202975, -0.2588190451025214056 ) ) ;
#52058=CARTESIAN_POINT ( 'NONE',  ( 51.18398860626899705, 28.73617430169823095, 5.000000000000000000 ) ) ;
#52061=ORIENTED_EDGE ( 'NONE', *, *, #114565, .F. ) ;
#52062=FACE_OUTER_BOUND ( 'NONE', #52110, .T. ) ;
#52063=EDGE_CURVE ( 'NONE', #126052, #50012, #22834, .T. ) ;
#52064=DIRECTION ( 'NONE',  ( 1.000000000000000000, 0.000000000000000000, 0.000000000000000000 ) ) ;
#52065=ORIENTED_EDGE ( 'NONE', *, *, #88593, .T. ) ;
#52066=CARTESIAN_POINT ( 'NONE',  ( -4.171830600776436526, -2.240707523384257716, 4.000000000000000000 ) ) ;
#52067=LINE ( 'NONE', #30307, #141416 ) ;
#52068=ORIENTED_EDGE ( 'NONE', *, *, #74053, .T. ) ;
#52069=DIRECTION ( 'NONE',  ( 0.7071067811865486830, -0.7071067811865464625, -0.000000000000000000 ) ) ;
#52070=EDGE_CURVE ( 'NONE', #113191, #121130, #67104, .T. ) ;
#52071=DIRECTION ( 'NONE',  ( 0.000000000000000000, -0.3543493200069152138, 0.9351131265310292928 ) ) ;
#52072=ORIENTED_EDGE ( 'NONE', *, *, #108289, .T. ) ;
#52075=ORIENTED_EDGE ( 'NONE', *, *, #75822, .F. ) ;
#52076=CARTESIAN_POINT ( 'NONE',  ( -14.33153258840134292, -18.74070752338409207, 20.73178291233837811 ) ) ;
#52079=LINE ( 'NONE', #65854, #29962 ) ;
#52080=FACE_OUTER_BOUND ( 'NONE', #6379, .T. ) ;
#52081=CARTESIAN_POINT ( 'NONE',  ( 24.47336096364199420, -5.240707523384228850, 16.25846745537501548 ) ) ;
#52082=LINE ( 'NONE', #140503, #34472 ) ;
#52086=LINE ( 'NONE', #39067, #64055 ) ;
#52087=EDGE_LOOP ( 'NONE', ( #56039, #82798, #78565, #72947, #10243 ) ) ;
#52088=VERTEX_POINT ( 'NONE', #24302 ) ;
#52089=EDGE_LOOP ( 'NONE', ( #64005, #78869, #52463, #15085 ) ) ;
#52090=LINE ( 'NONE', #96268, #129063 ) ;
#52091=LINE ( 'NONE', #65868, #78636 ) ;
#52094=ORIENTED_EDGE ( 'NONE', *, *, #58339, .T. ) ;
#52095=CARTESIAN_POINT ( 'NONE',  ( 18.18398860626898994, 28.73617430169800002, 5.000000000000000000 ) ) ;
#52096=LINE ( 'NONE', #74584, #102113 ) ;
#52099=LINE ( 'NONE', #30346, #19706 ) ;
#52100=ORIENTED_EDGE ( 'NONE', *, *, #41368, .F. ) ;
#52103=CARTESIAN_POINT ( 'NONE',  ( -19.02459472929562878, 22.22500000000000142, 11.02525794543162263 ) ) ;
#52104=CARTESIAN_POINT ( 'NONE',  ( 0.000000000000000000, 0.000000000000000000, 5.000000000000000000 ) ) ;
#52105=CARTESIAN_POINT ( 'NONE',  ( 0.000000000000000000, 0.000000000000000000, 5.000000000000000000 ) ) ;
#52107=ORIENTED_EDGE ( 'NONE', *, *, #28548, .F. ) ;
#52109=ORIENTED_EDGE ( 'NONE', *, *, #75762, .T. ) ;
#52110=EDGE_LOOP ( 'NONE', ( #90592, #127318, #57001, #33733 ) ) ;
#52112=ORIENTED_EDGE ( 'NONE', *, *, #33371, .T. ) ;
#52113=VECTOR ( 'NONE', #12150, 1000.000000000000000 ) ;
#52115=LINE ( 'NONE', #74605, #6332 ) ;
#52116=ORIENTED_EDGE ( 'NONE', *, *, #13493, .F. ) ;
#52117=PLANE ( 'NONE',  #74531 ) ;
#52118=PLANE ( 'NONE',  #118316 ) ;
#52123=VECTOR ( 'NONE', #39300, 1000.000000000000000 ) ;
#52124=CARTESIAN_POINT ( 'NONE',  ( -57.48921356237308800, -27.52281430457095368, 5.000000000000000000 ) ) ;
#52125=CARTESIAN_POINT ( 'NONE',  ( 30.18398860626900060, 28.73617430169808173, 5.000000000000000000 ) ) ;
#52126=DIRECTION ( 'NONE',  ( 0.7071067811865487940, 0.7071067811865463515, -0.000000000000000000 ) ) ;
#52127=CARTESIAN_POINT ( 'NONE',  ( 30.81349135397619676, -15.74070752338412760, 8.904080028138867675 ) ) ;
#52128=ORIENTED_EDGE ( 'NONE', *, *, #4292, .T. ) ;
#52129=EDGE_LOOP ( 'NONE', ( #57687, #41762, #109214, #25608 ) ) ;
#52131=ORIENTED_EDGE ( 'NONE', *, *, #63822, .T. ) ;
#52132=CARTESIAN_POINT ( 'NONE',  ( 37.21321903303336143, 12.75929247661558996, 10.29404684609044018 ) ) ;
#52133=ADVANCED_FACE ( 'NONE', ( #12691 ), #35209, .F. ) ;
#52134=CARTESIAN_POINT ( 'NONE',  ( 31.82816939922330945, 9.759292476615621936, 4.000000000000000000 ) ) ;
#52139=VECTOR ( 'NONE', #130858, 1000.000000000000000 ) ;
#52140=EDGE_LOOP ( 'NONE', ( #1578, #111029, #58321, #79278, #138681 ) ) ;
#52141=AXIS2_PLACEMENT_3D ( 'NONE', #99652, #119707, #47242 ) ;
#52142=EDGE_CURVE ( 'NONE', #73921, #75761, #38051, .T. ) ;
#52144=VERTEX_POINT ( 'NONE', #5377 ) ;
#52145=VERTEX_POINT ( 'NONE', #117694 ) ;
#52146=EDGE_CURVE ( 'NONE', #47459, #109538, #115548, .T. ) ;
#52147=DIRECTION ( 'NONE',  ( -0.000000000000000000, -0.3543493200069152693, 0.9351131265310292928 ) ) ;
#52148=CARTESIAN_POINT ( 'NONE',  ( -4.499999999999966249, -16.53360074219757081, 5.000000000000000000 ) ) ;
#52149=ORIENTED_EDGE ( 'NONE', *, *, #59628, .F. ) ;
#52150=PLANE ( 'NONE',  #127017 ) ;
#52152=DIRECTION ( 'NONE',  ( 0.000000000000000000, 1.000000000000000000, 0.000000000000000000 ) ) ;
#52153=LINE ( 'NONE', #97040, #101565 ) ;
#52155=EDGE_CURVE ( 'NONE', #46584, #73005, #139528, .T. ) ;
#52156=EDGE_LOOP ( 'NONE', ( #142644, #48032, #103961, #86913 ) ) ;
#52157=CARTESIAN_POINT ( 'NONE',  ( -8.207106781186485733, 12.75929247661559351, 5.000000000000000000 ) ) ;
#52158=FACE_BOUND ( 'NONE', #24947, .T. ) ;
#52160=CARTESIAN_POINT ( 'NONE',  ( 34.49999999999975842, 19.46425560840029689, 4.994342998332160555 ) ) ;
#52162=LINE ( 'NONE', #107935, #134916 ) ;
#52163=ORIENTED_EDGE ( 'NONE', *, *, #132488, .T. ) ;
#52164=CARTESIAN_POINT ( 'NONE',  ( -30.29974487139158867, -27.71228299555227537, 4.000000000000000000 ) ) ;
#52166=EDGE_LOOP ( 'NONE', ( #91588, #80910, #93340, #23574, #94598, #33502 ) ) ;
#52167=ORIENTED_EDGE ( 'NONE', *, *, #133650, .F. ) ;
#52170=DIRECTION ( 'NONE',  ( -0.6830127018922181881, 0.6830127018922202975, -0.2588190451025214056 ) ) ;
#52172=EDGE_CURVE ( 'NONE', #116772, #27223, #61270, .T. ) ;
#52173=FACE_OUTER_BOUND ( 'NONE', #13104, .T. ) ;
#52175=CARTESIAN_POINT ( 'NONE',  ( -56.99451991528749062, 28.92564299267978001, 4.000000000000000000 ) ) ;
#52177=EDGE_CURVE ( 'NONE', #23024, #33945, #29288, .T. ) ;
#52178=DIRECTION ( 'NONE',  ( -0.6830127018922181881, 0.6830127018922202975, -0.2588190451025214056 ) ) ;
#52179=CARTESIAN_POINT ( 'NONE',  ( -34.45011844616455221, -11.99769585840591724, 5.000000000000000888 ) ) ;
#52180=DIRECTION ( 'NONE',  ( -0.7071067811865487940, 0.7071067811865463515, 0.000000000000000000 ) ) ;
#52181=ORIENTED_EDGE ( 'NONE', *, *, #35424, .F. ) ;
#52182=VERTEX_POINT ( 'NONE', #137360 ) ;
#52183=EDGE_LOOP ( 'NONE', ( #112218, #108199, #11980, #8512 ) ) ;
#52184=VERTEX_POINT ( 'NONE', #104710 ) ;
#52185=CARTESIAN_POINT ( 'NONE',  ( 30.15612307739221265, -22.22500000000000142, 4.000000000000000000 ) ) ;
#52186=ORIENTED_EDGE ( 'NONE', *, *, #99245, .F. ) ;
#52187=EDGE_CURVE ( 'NONE', #64560, #79180, #138793, .T. ) ;
#52188=VERTEX_POINT ( 'NONE', #38749 ) ;
#52189=DIRECTION ( 'NONE',  ( 1.000000000000000000, 0.000000000000000000, 0.000000000000000000 ) ) ;
#52190=FACE_OUTER_BOUND ( 'NONE', #32858, .T. ) ;
#52192=EDGE_CURVE ( 'NONE', #117439, #122913, #136617, .T. ) ;
#52193=LINE ( 'NONE', #127628, #94812 ) ;
#52195=CARTESIAN_POINT ( 'NONE',  ( -14.99999999999989342, -3.033600742197705369, 5.000000000000000000 ) ) ;
#52196=ORIENTED_EDGE ( 'NONE', *, *, #91676, .T. ) ;
#52198=VECTOR ( 'NONE', #40893, 1000.000000000000000 ) ;
#52199=CARTESIAN_POINT ( 'NONE',  ( 15.67180000000000639, 3.174999999999997602, 5.000000000000000000 ) ) ;
#52200=EDGE_CURVE ( 'NONE', #89639, #89080, #126451, .T. ) ;
#52204=EDGE_CURVE ( 'NONE', #63895, #119902, #81570, .T. ) ;
#52205=DIRECTION ( 'NONE',  ( -0.000000000000000000, -0.3543493200069152693, 0.9351131265310292928 ) ) ;
#52206=VECTOR ( 'NONE', #92399, 1000.000000000000000 ) ;
#52207=LINE ( 'NONE', #53653, #111160 ) ;
#52208=PLANE ( 'NONE',  #102085 ) ;
#52209=ORIENTED_EDGE ( 'NONE', *, *, #70841, .F. ) ;
#52210=EDGE_LOOP ( 'NONE', ( #135770, #104324, #133197, #84883 ) ) ;
#52211=PLANE ( 'NONE',  #93643 ) ;
#52214=CARTESIAN_POINT ( 'NONE',  ( 23.99999999999983658, 14.96639925780211122, 5.000000000000000000 ) ) ;
#52215=EDGE_CURVE ( 'NONE', #111091, #35748, #28602, .T. ) ;
#52216=LINE ( 'NONE', #107305, #54354 ) ;
#52217=CARTESIAN_POINT ( 'NONE',  ( -13.49999999999990052, -9.462702396501018853, -9.474982329943482995 ) ) ;
#52218=EDGE_LOOP ( 'NONE', ( #51645, #75878, #65262, #111126 ) ) ;
#52219=LINE ( 'NONE', #76866, #99263 ) ;
#52220=VECTOR ( 'NONE', #78123, 999.9999999999998863 ) ;
#52221=LINE ( 'NONE', #39960, #58267 ) ;
#52222=CARTESIAN_POINT ( 'NONE',  ( -12.79289321881336328, 18.75929247661552068, 5.000000000000000000 ) ) ;
#52223=ORIENTED_EDGE ( 'NONE', *, *, #125074, .F. ) ;
#52226=VERTEX_POINT ( 'NONE', #73531 ) ;
#52227=DIRECTION ( 'NONE',  ( 0.7071067811865486830, -0.7071067811865464625, -0.000000000000000000 ) ) ;
#52228=VERTEX_POINT ( 'NONE', #117012 ) ;
#52229=ORIENTED_EDGE ( 'NONE', *, *, #21298, .F. ) ;
#52230=CARTESIAN_POINT ( 'NONE',  ( 20.99451991528748707, 28.92564299267952777, 4.000000000000000000 ) ) ;
#52231=DIRECTION ( 'NONE',  ( 1.000000000000000000, -0.000000000000000000, 0.000000000000000000 ) ) ;
#52232=EDGE_CURVE ( 'NONE', #124219, #63953, #17679, .T. ) ;
#52233=EDGE_LOOP ( 'NONE', ( #106735, #60961, #92424, #72392 ) ) ;
#52235=VECTOR ( 'NONE', #11248, 1000.000000000000000 ) ;
#52236=EDGE_CURVE ( 'NONE', #57178, #98347, #27148, .T. ) ;
#52239=VECTOR ( 'NONE', #28224, 999.9999999999998863 ) ;
#52240=LINE ( 'NONE', #19608, #20648 ) ;
#52241=VECTOR ( 'NONE', #13129, 1000.000000000000000 ) ;
#52242=CARTESIAN_POINT ( 'NONE',  ( 21.79289321881331176, -20.24070752338407431, 5.000000000000000000 ) ) ;
#52244=CARTESIAN_POINT ( 'NONE',  ( -42.48921356237308800, -27.52281430457085065, 5.000000000000000000 ) ) ;
#52245=DIRECTION ( 'NONE',  ( 0.3543493200069162685, -0.000000000000000000, -0.9351131265310288487 ) ) ;
#52246=CARTESIAN_POINT ( 'NONE',  ( -31.49999999999977973, -7.912538124160673370, 4.000000000000000000 ) ) ;
#52247=CARTESIAN_POINT ( 'NONE',  ( 8.292986735706890045, -21.74070752338406365, 4.999753212805221558 ) ) ;
#52248=CARTESIAN_POINT ( 'NONE',  ( 42.48921356237308800, -27.52281430457085065, 5.000000000000000000 ) ) ;
#52249=DIRECTION ( 'NONE',  ( -0.7071067811865486830, -0.7071067811865464625, 0.000000000000000000 ) ) ;
#52250=EDGE_CURVE ( 'NONE', #121222, #33858, #93836, .T. ) ;
#52251=CARTESIAN_POINT ( 'NONE',  ( 0.000000000000000000, 0.000000000000000000, 5.000000000000000000 ) ) ;
#52252=ORIENTED_EDGE ( 'NONE', *, *, #68574, .F. ) ;
#52253=EDGE_LOOP ( 'NONE', ( #39891, #105164, #64179, #53044 ) ) ;
#52254=EDGE_LOOP ( 'NONE', ( #11083, #63103, #125840, #124047 ) ) ;
#52256=ORIENTED_EDGE ( 'NONE', *, *, #86407, .F. ) ;
#52257=EDGE_LOOP ( 'NONE', ( #127169, #70294, #49649, #83917 ) ) ;
#52260=DIRECTION ( 'NONE',  ( -0.6830127018922180770, -0.6830127018922204085, -0.2588190451025213501 ) ) ;
#52261=ORIENTED_EDGE ( 'NONE', *, *, #81942, .F. ) ;
#52262=LINE ( 'NONE', #27645, #106332 ) ;
#52263=CARTESIAN_POINT ( 'NONE',  ( -34.92500000000001137, -22.22500000000000142, 4.000000000000000000 ) ) ;
#52264=LINE ( 'NONE', #117497, #132030 ) ;
#52265=CARTESIAN_POINT ( 'NONE',  ( -18.18398860626898994, 28.73617430169800002, 5.000000000000000000 ) ) ;
#52267=ORIENTED_EDGE ( 'NONE', *, *, #56005, .T. ) ;
#52268=CARTESIAN_POINT ( 'NONE',  ( 11.29289321881338459, -3.740707523384243505, 5.000000000000000000 ) ) ;
#52270=CARTESIAN_POINT ( 'NONE',  ( -15.56584921360887108, 8.021612662230191759, 4.000000000000000000 ) ) ;
#52271=PLANE ( 'NONE',  #111834 ) ;
#52275=DIRECTION ( 'NONE',  ( 0.7071067811865487940, 0.7071067811865463515, -0.000000000000000000 ) ) ;
#52277=ORIENTED_EDGE ( 'NONE', *, *, #60727, .F. ) ;
#52279=ORIENTED_EDGE ( 'NONE', *, *, #2155, .F. ) ;
#52280=LINE ( 'NONE', #7329, #34783 ) ;
#52282=DIRECTION ( 'NONE',  ( -1.000000000000000000, 0.000000000000000000, 0.000000000000000000 ) ) ;
#52283=DIRECTION ( 'NONE',  ( -0.6830127018922180770, -0.6830127018922204085, -0.2588190451025213501 ) ) ;
#52284=CARTESIAN_POINT ( 'NONE',  ( -3.005480084712505828, 28.92564299267936079, 4.000000000000000000 ) ) ;
#52285=CARTESIAN_POINT ( 'NONE',  ( -17.29289321881333308, -12.74070752338415247, 5.000000000000000000 ) ) ;
#52286=CARTESIAN_POINT ( 'NONE',  ( -30.32816939922332367, 20.25929247661551003, 4.000000000000000000 ) ) ;
#52288=ORIENTED_EDGE ( 'NONE', *, *, #34345, .T. ) ;
#52289=DIRECTION ( 'NONE',  ( -0.000000000000000000, 0.3543493200069152138, -0.9351131265310292928 ) ) ;
#52291=DIRECTION ( 'NONE',  ( -0.3543493200069162685, -0.000000000000000000, -0.9351131265310288487 ) ) ;
#52294=EDGE_CURVE ( 'NONE', #40982, #25852, #130784, .T. ) ;
#52295=PLANE ( 'NONE',  #27913 ) ;
#52296=ORIENTED_EDGE ( 'NONE', *, *, #109651, .F. ) ;
#52298=EDGE_CURVE ( 'NONE', #74460, #56797, #53939, .T. ) ;
#52300=DIRECTION ( 'NONE',  ( 0.3543493200069162685, -0.000000000000000000, -0.9351131265310288487 ) ) ;
#52301=CARTESIAN_POINT ( 'NONE',  ( 6.291777089830439706, -15.74070752338412404, 19.73771281079099182 ) ) ;
#52302=CARTESIAN_POINT ( 'NONE',  ( 11.24139925780195171, 21.72500000000000142, 5.000000000000000000 ) ) ;
#52303=CARTESIAN_POINT ( 'NONE',  ( 35.90156419391741593, 11.25929247661559884, 10.79108189686415642 ) ) ;
#52305=EDGE_CURVE ( 'NONE', #107270, #127430, #19134, .T. ) ;
#52306=EDGE_CURVE ( 'NONE', #79941, #124966, #87963, .T. ) ;
#52307=AXIS2_PLACEMENT_3D ( 'NONE', #20025, #140397, #21485 ) ;
#52309=ORIENTED_EDGE ( 'NONE', *, *, #68411, .T. ) ;
#52310=EDGE_CURVE ( 'NONE', #42625, #6455, #131477, .T. ) ;
#52311=CARTESIAN_POINT ( 'NONE',  ( -17.99999999999986855, -15.41253812416059965, 4.000000000000000000 ) ) ;
#52312=ORIENTED_EDGE ( 'NONE', *, *, #65798, .T. ) ;
#52313=ORIENTED_EDGE ( 'NONE', *, *, #19102, .T. ) ;
#52316=CARTESIAN_POINT ( 'NONE',  ( 25.49999999999982947, 22.22500000000000142, 4.362957392718778138 ) ) ;
#52318=VERTEX_POINT ( 'NONE', #42343 ) ;
#52320=AXIS2_PLACEMENT_3D ( 'NONE', #132354, #77258, #111252 ) ;
#52322=EDGE_CURVE ( 'NONE', #12211, #44871, #29999, .T. ) ;
#52323=FACE_OUTER_BOUND ( 'NONE', #89185, .T. ) ;
#52324=FACE_BOUND ( 'NONE', #94238, .T. ) ;
#52325=ORIENTED_EDGE ( 'NONE', *, *, #142645, .F. ) ;
#52326=CARTESIAN_POINT ( 'NONE',  ( 33.79289321881321939, 18.75929247661552779, 5.000000000000000000 ) ) ;
#52327=DIRECTION ( 'NONE',  ( -0.7071067811865487940, 0.7071067811865463515, -0.000000000000000000 ) ) ;
#52328=CARTESIAN_POINT ( 'NONE',  ( -60.18398860626900415, 28.73617430169829490, 5.000000000000000000 ) ) ;
#52329=VERTEX_POINT ( 'NONE', #142360 ) ;
#52330=LINE ( 'NONE', #117561, #55045 ) ;
#52331=EDGE_LOOP ( 'NONE', ( #75587, #59341, #82694, #50336 ) ) ;
#52332=EDGE_CURVE ( 'NONE', #48062, #52188, #98135, .T. ) ;
#52334=DIRECTION ( 'NONE',  ( 0.3543493200069162685, -0.000000000000000000, -0.9351131265310288487 ) ) ;
#52335=VECTOR ( 'NONE', #9670, 1000.000000000000000 ) ;
#52336=ORIENTED_EDGE ( 'NONE', *, *, #23372, .T. ) ;
#52340=LINE ( 'NONE', #108120, #39534 ) ;
#52341=AXIS2_PLACEMENT_3D ( 'NONE', #46448, #81189, #79798 ) ;
#52342=LINE ( 'NONE', #17562, #93594 ) ;
#52343=EDGE_CURVE ( 'NONE', #89978, #10977, #119842, .T. ) ;
#52344=ORIENTED_EDGE ( 'NONE', *, *, #61392, .T. ) ;
#52348=DIRECTION ( 'NONE',  ( -0.7071067811865486830, -0.7071067811865464625, -0.000000000000000000 ) ) ;
#52349=CARTESIAN_POINT ( 'NONE',  ( 19.49999999999986500, -17.91344420646041158, 1.358650452708509038 ) ) ;
#52350=DIRECTION ( 'NONE',  ( 1.000000000000000000, 0.000000000000000000, 0.000000000000000000 ) ) ;
#52351=EDGE_CURVE ( 'NONE', #143094, #68410, #40895, .T. ) ;
#52352=LINE ( 'NONE', #21152, #67971 ) ;
#52353=DIRECTION ( 'NONE',  ( 0.7071067811865487940, 0.7071067811865463515, 0.000000000000000000 ) ) ;
#52354=VERTEX_POINT ( 'NONE', #8221 ) ;
#52355=ORIENTED_EDGE ( 'NONE', *, *, #78901, .F. ) ;
#52356=CARTESIAN_POINT ( 'NONE',  ( 1.734933297179483525, 12.75929247661558996, 18.34774599283955965 ) ) ;
#52357=DIRECTION ( 'NONE',  ( -0.3543493200069162685, -0.000000000000000000, -0.9351131265310288487 ) ) ;
#52358=ORIENTED_EDGE ( 'NONE', *, *, #11409, .T. ) ;
#52360=EDGE_LOOP ( 'NONE', ( #51791, #110695, #130234, #139246 ) ) ;
#52361=VERTEX_POINT ( 'NONE', #10383 ) ;
#52362=FACE_OUTER_BOUND ( 'NONE', #57365, .T. ) ;
#52363=CARTESIAN_POINT ( 'NONE',  ( -1.499999999999994449, 19.08746187583905751, 4.000000000000000000 ) ) ;
#52364=FACE_OUTER_BOUND ( 'NONE', #91303, .T. ) ;
#52365=EDGE_LOOP ( 'NONE', ( #36980, #109427, #124148, #110099, #81275 ) ) ;
#52366=CARTESIAN_POINT ( 'NONE',  ( -42.29974487139158157, -27.71228299555235708, 4.000000000000000000 ) ) ;
#52367=DIRECTION ( 'NONE',  ( 0.7071067811865486830, -0.7071067811865464625, -0.000000000000000000 ) ) ;
#52369=DIRECTION ( 'NONE',  ( -0.7071067811865486830, -0.7071067811865464625, 0.000000000000000000 ) ) ;
#52370=EDGE_LOOP ( 'NONE', ( #2094, #1226, #9522, #3343 ) ) ;
#52374=DIRECTION ( 'NONE',  ( 0.7071067811865487940, 0.7071067811865463515, 0.000000000000000000 ) ) ;
#52376=ORIENTED_EDGE ( 'NONE', *, *, #60401, .T. ) ;
#52378=FACE_OUTER_BOUND ( 'NONE', #124083, .T. ) ;
#52380=CARTESIAN_POINT ( 'NONE',  ( 34.92499999999998295, 13.70193056682084887, 4.500000000000000888 ) ) ;
#52382=DIRECTION ( 'NONE',  ( 0.7071067811865487940, 0.7071067811865463515, -0.000000000000000000 ) ) ;
#52384=EDGE_LOOP ( 'NONE', ( #9123, #33563, #5978, #123495 ) ) ;
#52385=PLANE ( 'NONE',  #95827 ) ;
#52386=CARTESIAN_POINT ( 'NONE',  ( -33.48921356237309510, -27.52281430457078670, 5.000000000000000000 ) ) ;
#52388=VECTOR ( 'NONE', #26411, 1000.000000000000000 ) ;
#52389=ORIENTED_EDGE ( 'NONE', *, *, #89007, .T. ) ;
#52390=CARTESIAN_POINT ( 'NONE',  ( -31.82816939922330945, -5.240707523384227073, 4.000000000000000000 ) ) ;
#52391=CARTESIAN_POINT ( 'NONE',  ( 16.49999999999987566, 8.319652575858389909, -8.582050562765786594 ) ) ;
#52392=FACE_OUTER_BOUND ( 'NONE', #17121, .T. ) ;
#52393=LINE ( 'NONE', #86477, #20702 ) ;
#52394=VERTEX_POINT ( 'NONE', #95969 ) ;
#52396=FACE_OUTER_BOUND ( 'NONE', #76764, .T. ) ;
#52397=CARTESIAN_POINT ( 'NONE',  ( 31.49999999999977973, 8.900465351122178959, -2.516491619111585809 ) ) ;
#52399=VECTOR ( 'NONE', #62004, 1000.000000000000000 ) ;
#52401=EDGE_CURVE ( 'NONE', #117130, #25131, #64182, .T. ) ;
#52402=FACE_OUTER_BOUND ( 'NONE', #87843, .T. ) ;
#52403=DIRECTION ( 'NONE',  ( 0.6830127018922180770, -0.6830127018922204085, -0.2588190451025213501 ) ) ;
#52404=VECTOR ( 'NONE', #39687, 1000.000000000000000 ) ;
#52405=ORIENTED_EDGE ( 'NONE', *, *, #114159, .T. ) ;
#52407=CARTESIAN_POINT ( 'NONE',  ( 23.20710678118638270, -17.24070752338410628, 5.000000000000000000 ) ) ;
#52408=CARTESIAN_POINT ( 'NONE',  ( 60.18398860626900415, 28.73617430169829490, 5.000000000000000000 ) ) ;
#52409=DIRECTION ( 'NONE',  ( 1.000000000000000000, 0.000000000000000000, 0.000000000000000000 ) ) ;
#52411=DIRECTION ( 'NONE',  ( -1.000000000000000000, 6.248375730189539568E-15, 0.000000000000000000 ) ) ;
#52412=VERTEX_POINT ( 'NONE', #111868 ) ;
#52413=CARTESIAN_POINT ( 'NONE',  ( 33.79289321881321939, -5.240707523384228850, 5.000000000000000000 ) ) ;
#52414=ORIENTED_EDGE ( 'NONE', *, *, #104940, .F. ) ;
#52417=LINE ( 'NONE', #96602, #89542 ) ;
#52418=CARTESIAN_POINT ( 'NONE',  ( 29.99999999999979394, -6.108550654416931458, -3.114665004254898673 ) ) ;
#52421=LINE ( 'NONE', #96606, #46576 ) ;
#52422=CARTESIAN_POINT ( 'NONE',  ( 0.000000000000000000, 0.000000000000000000, 5.000000000000000000 ) ) ;
#52423=VECTOR ( 'NONE', #1112, 1000.000000000000000 ) ;
#52424=PLANE ( 'NONE',  #53425 ) ;
#52425=CARTESIAN_POINT ( 'NONE',  ( 7.828169399223476432, -11.24070752338416135, 4.000000000000000000 ) ) ;
#52426=ORIENTED_EDGE ( 'NONE', *, *, #35654, .F. ) ;
#52428=FACE_OUTER_BOUND ( 'NONE', #51533, .T. ) ;
#52429=FACE_OUTER_BOUND ( 'NONE', #10560, .T. ) ;
#52430=CARTESIAN_POINT ( 'NONE',  ( 8.999999999999941380, 4.965500833774342482, -4.007596771432676341 ) ) ;
#52431=AXIS2_PLACEMENT_3D ( 'NONE', #139359, #64615, #7355 ) ;
#52432=CARTESIAN_POINT ( 'NONE',  ( 34.45011844616451668, 6.002304141593879372, 5.000000000000000888 ) ) ;
#52433=VECTOR ( 'NONE', #140223, 1000.000000000000000 ) ;
#52435=VECTOR ( 'NONE', #107390, 1000.000000000000000 ) ;
#52437=VERTEX_POINT ( 'NONE', #132934 ) ;
#52438=ORIENTED_EDGE ( 'NONE', *, *, #16138, .T. ) ;
#52439=VECTOR ( 'NONE', #14954, 1000.000000000000227 ) ;
#52441=CARTESIAN_POINT ( 'NONE',  ( 21.48921356237309155, -27.52281430457070499, 5.000000000000000000 ) ) ;
#52444=CARTESIAN_POINT ( 'NONE',  ( -33.29974487139158867, -27.71228299555229313, 4.000000000000000000 ) ) ;
#52445=ORIENTED_EDGE ( 'NONE', *, *, #73936, .F. ) ;
#52446=DIRECTION ( 'NONE',  ( 0.7071067811865486830, -0.7071067811865464625, -0.000000000000000000 ) ) ;
#52450=DIRECTION ( 'NONE',  ( 0.3543493200069162685, -0.000000000000000000, -0.9351131265310288487 ) ) ;
#52451=ORIENTED_EDGE ( 'NONE', *, *, #103654, .T. ) ;
#52452=ORIENTED_EDGE ( 'NONE', *, *, #19130, .F. ) ;
#52454=LINE ( 'NONE', #120543, #66234 ) ;
#52455=CARTESIAN_POINT ( 'NONE',  ( -34.92500000000001137, -17.99387692260789251, 4.000000000000000000 ) ) ;
#52456=EDGE_CURVE ( 'NONE', #121050, #42538, #80675, .T. ) ;
#52457=CARTESIAN_POINT ( 'NONE',  ( -69.18398860626899705, 28.73617430169835529, 5.000000000000000000 ) ) ;
#52458=ORIENTED_EDGE ( 'NONE', *, *, #140060, .F. ) ;
#52459=LINE ( 'NONE', #140891, #14143 ) ;
#52460=EDGE_CURVE ( 'NONE', #89130, #126442, #46658, .T. ) ;
#52461=EDGE_CURVE ( 'NONE', #111700, #40790, #135760, .T. ) ;
#52463=ORIENTED_EDGE ( 'NONE', *, *, #13326, .F. ) ;
#52465=LINE ( 'NONE', #63395, #119473 ) ;
#52466=LINE ( 'NONE', #140898, #93471 ) ;
#52467=FACE_OUTER_BOUND ( 'NONE', #49591, .T. ) ;
#52468=EDGE_CURVE ( 'NONE', #24662, #11839, #88697, .T. ) ;
#52469=ORIENTED_EDGE ( 'NONE', *, *, #4826, .F. ) ;
#52470=EDGE_CURVE ( 'NONE', #50212, #57095, #133621, .T. ) ;
#52471=ORIENTED_EDGE ( 'NONE', *, *, #52920, .F. ) ;
#52472=VECTOR ( 'NONE', #31176, 1000.000000000000000 ) ;
#52473=FACE_OUTER_BOUND ( 'NONE', #51034, .T. ) ;
#52475=CARTESIAN_POINT ( 'NONE',  ( -0.4892135623730947680, -27.52281430457055578, 5.000000000000000000 ) ) ;
#52476=EDGE_CURVE ( 'NONE', #25093, #70259, #79987, .T. ) ;
#52477=CARTESIAN_POINT ( 'NONE',  ( 27.18398860626900060, 28.73617430169806042, 5.000000000000000000 ) ) ;
#52478=CARTESIAN_POINT ( 'NONE',  ( -18.48921356237309510, -27.52281430457068367, 5.000000000000000000 ) ) ;
#52480=ORIENTED_EDGE ( 'NONE', *, *, #138282, .T. ) ;
#52481=VECTOR ( 'NONE', #52282, 1000.000000000000000 ) ;
#52482=EDGE_CURVE ( 'NONE', #82894, #80563, #58247, .T. ) ;
#52484=DIRECTION ( 'NONE',  ( -0.6830127018922180770, -0.6830127018922204085, -0.2588190451025213501 ) ) ;
#52485=ORIENTED_EDGE ( 'NONE', *, *, #68236, .F. ) ;
#52486=EDGE_CURVE ( 'NONE', #94514, #115757, #24843, .T. ) ;
#52487=ORIENTED_EDGE ( 'NONE', *, *, #95735, .T. ) ;
#52488=LINE ( 'NONE', #75691, #141662 ) ;
#52489=EDGE_LOOP ( 'NONE', ( #141374, #98419, #93324, #15011 ) ) ;
#52490=CARTESIAN_POINT ( 'NONE',  ( 0.000000000000000000, 0.000000000000000000, 5.000000000000000000 ) ) ;
#52491=PLANE ( 'NONE',  #54941 ) ;
#52493=ADVANCED_FACE ( 'NONE', ( #45909 ), #33611, .F. ) ;
#52494=DIRECTION ( 'NONE',  ( 0.6830127018922181881, 0.6830127018922202975, -0.2588190451025214056 ) ) ;
#52495=AXIS2_PLACEMENT_3D ( 'NONE', #82653, #27527, #73910 ) ;
#52496=FACE_BOUND ( 'NONE', #122840, .T. ) ;
#52497=DIRECTION ( 'NONE',  ( 1.000000000000000000, 0.000000000000000000, 0.000000000000000000 ) ) ;
#52499=DIRECTION ( 'NONE',  ( -0.7071067811865486830, -0.7071067811865464625, 0.000000000000000000 ) ) ;
#52500=FACE_OUTER_BOUND ( 'NONE', #114413, .T. ) ;
#52501=ORIENTED_EDGE ( 'NONE', *, *, #25250, .T. ) ;
#52505=VECTOR ( 'NONE', #51657, 1000.000000000000000 ) ;
#52509=ORIENTED_EDGE ( 'NONE', *, *, #89886, .T. ) ;
#52511=CARTESIAN_POINT ( 'NONE',  ( -17.29289321881334018, 17.25929247661554200, 5.000000000000000000 ) ) ;
#52512=ADVANCED_FACE ( 'NONE', ( #11078 ), #55351, .T. ) ;
#52513=EDGE_LOOP ( 'NONE', ( #20948, #34710, #103495, #7855 ) ) ;
#52514=LINE ( 'NONE', #95304, #9705 ) ;
#52515=CARTESIAN_POINT ( 'NONE',  ( 13.08100000000000307, 3.174999999999998046, 1.444000000000000394 ) ) ;
#52516=ADVANCED_FACE ( 'NONE', ( #56089 ), #929, .F. ) ;
#52517=CARTESIAN_POINT ( 'NONE',  ( -24.70710678118637915, 17.25929247661554911, 5.000000000000000000 ) ) ;
#52518=DIRECTION ( 'NONE',  ( 0.6830127018922180770, -0.6830127018922204085, -0.2588190451025213501 ) ) ;
#52519=DIRECTION ( 'NONE',  ( 0.3543493200069162685, -0.000000000000000000, -0.9351131265310288487 ) ) ;
#52520=EDGE_CURVE ( 'NONE', #115378, #104397, #79282, .T. ) ;
#52521=CARTESIAN_POINT ( 'NONE',  ( 0.000000000000000000, 0.000000000000000000, 5.000000000000000000 ) ) ;
#52522=CARTESIAN_POINT ( 'NONE',  ( 21.48921356237309155, -27.52281430457070499, 5.000000000000000000 ) ) ;
#52524=CARTESIAN_POINT ( 'NONE',  ( 34.92499999999998295, 6.662461875838954661, 4.000000000000000000 ) ) ;
#52525=ORIENTED_EDGE ( 'NONE', *, *, #26465, .F. ) ;
#52526=LINE ( 'NONE', #95319, #109744 ) ;
#52527=EDGE_CURVE ( 'NONE', #82948, #80191, #123484, .T. ) ;
#52529=EDGE_CURVE ( 'NONE', #80080, #68527, #68392, .T. ) ;
#52530=VERTEX_POINT ( 'NONE', #50894 ) ;
#52531=VECTOR ( 'NONE', #79292, 1000.000000000000000 ) ;
#52532=VERTEX_POINT ( 'NONE', #114693 ) ;
#52533=ORIENTED_EDGE ( 'NONE', *, *, #35017, .F. ) ;
#52535=ORIENTED_EDGE ( 'NONE', *, *, #28442, .F. ) ;
#52537=VECTOR ( 'NONE', #17023, 1000.000000000000000 ) ;
#52538=VECTOR ( 'NONE', #27518, 1000.000000000000227 ) ;
#52539=VECTOR ( 'NONE', #35022, 1000.000000000000227 ) ;
#52542=ORIENTED_EDGE ( 'NONE', *, *, #84770, .F. ) ;
#52544=CARTESIAN_POINT ( 'NONE',  ( -20.99999999999985079, -12.03360074219761344, 5.000000000000000000 ) ) ;
#52545=VECTOR ( 'NONE', #56383, 1000.000000000000000 ) ;
#52546=ORIENTED_EDGE ( 'NONE', *, *, #131323, .F. ) ;
#52547=DIRECTION ( 'NONE',  ( 0.000000000000000000, 1.000000000000000000, 0.000000000000000000 ) ) ;
#52548=CARTESIAN_POINT ( 'NONE',  ( 63.48921356237309510, -27.52281430457099631, 5.000000000000000000 ) ) ;
#52549=CARTESIAN_POINT ( 'NONE',  ( 2.999999999999981792, -2.904428200921304271, -6.989807076074948000 ) ) ;
#52550=EDGE_LOOP ( 'NONE', ( #28052, #91922, #4510, #7861, #57978, #92111 ) ) ;
#52551=ORIENTED_EDGE ( 'NONE', *, *, #131964, .T. ) ;
#52552=LINE ( 'NONE', #96732, #35366 ) ;
#52553=DIRECTION ( 'NONE',  ( -0.6830127018922180770, -0.6830127018922204085, -0.2588190451025213501 ) ) ;
#52554=EDGE_LOOP ( 'NONE', ( #98077, #114643, #44863, #38269 ) ) ;
#52555=PLANE ( 'NONE',  #124554 ) ;
#52556=ORIENTED_EDGE ( 'NONE', *, *, #22328, .T. ) ;
#52557=EDGE_LOOP ( 'NONE', ( #80046, #37518, #26555, #26577 ) ) ;
#52558=EDGE_CURVE ( 'NONE', #3888, #138634, #39313, .T. ) ;
#52559=ORIENTED_EDGE ( 'NONE', *, *, #93787, .T. ) ;
#52560=CARTESIAN_POINT ( 'NONE',  ( -18.32816939922339472, -15.74070752338412760, 4.000000000000000000 ) ) ;
#52561=LINE ( 'NONE', #96744, #77106 ) ;
#52562=LINE ( 'NONE', #38313, #32982 ) ;
#52563=FACE_OUTER_BOUND ( 'NONE', #12611, .T. ) ;
#52564=EDGE_CURVE ( 'NONE', #140080, #23121, #58971, .T. ) ;
#52565=DIRECTION ( 'NONE',  ( 0.7071067811865487940, -0.7071067811865463515, 0.000000000000000000 ) ) ;
#52566=ORIENTED_EDGE ( 'NONE', *, *, #86450, .F. ) ;
#52567=DIRECTION ( 'NONE',  ( -0.7071067811865486830, 0.7071067811865464625, 0.000000000000000000 ) ) ;
#52569=ORIENTED_EDGE ( 'NONE', *, *, #11407, .F. ) ;
#52570=VECTOR ( 'NONE', #119396, 1000.000000000000000 ) ;
#52571=LINE ( 'NONE', #85919, #123490 ) ;
#52573=VECTOR ( 'NONE', #102517, 1000.000000000000000 ) ;
#52574=ORIENTED_EDGE ( 'NONE', *, *, #77923, .T. ) ;
#52575=DIRECTION ( 'NONE',  ( -0.7071067811865487940, 0.7071067811865463515, -0.000000000000000000 ) ) ;
#52577=ADVANCED_FACE ( 'NONE', ( #49499 ), #81406, .T. ) ;
#52578=ORIENTED_EDGE ( 'NONE', *, *, #41911, .F. ) ;
#52579=ORIENTED_EDGE ( 'NONE', *, *, #87439, .T. ) ;
#52580=PLANE ( 'NONE',  #6980 ) ;
#52581=DIRECTION ( 'NONE',  ( -0.7071067811865486830, -0.7071067811865464625, 0.000000000000000000 ) ) ;
#52582=LINE ( 'NONE', #41003, #33122 ) ;
#52584=CARTESIAN_POINT ( 'NONE',  ( -34.42500000000001137, -18.02281430457038880, 5.000000000000000000 ) ) ;
#52586=EDGE_CURVE ( 'NONE', #125809, #65260, #127747, .T. ) ;
#52587=FACE_BOUND ( 'NONE', #112272, .T. ) ;
#52588=LINE ( 'NONE', #31569, #48533 ) ;
#52589=ADVANCED_FACE ( 'NONE', ( #128458 ), #6608, .F. ) ;
#52590=CARTESIAN_POINT ( 'NONE',  ( 48.48921356237309510, -27.52281430457089328, 5.000000000000000000 ) ) ;
#52591=CARTESIAN_POINT ( 'NONE',  ( -17.99999999999987566, -13.06887692260767331, 4.000000000000000000 ) ) ;
#52592=VERTEX_POINT ( 'NONE', #61784 ) ;
#52593=CARTESIAN_POINT ( 'NONE',  ( -51.18398860626899705, 28.73617430169823095, 5.000000000000000000 ) ) ;
#52595=ORIENTED_EDGE ( 'NONE', *, *, #27974, .F. ) ;
#52596=LINE ( 'NONE', #122127, #87167 ) ;
#52599=PLANE ( 'NONE',  #13729 ) ;
#52600=DIRECTION ( 'NONE',  ( 0.7071067811865486830, -0.7071067811865464625, -0.000000000000000000 ) ) ;
#52601=ORIENTED_EDGE ( 'NONE', *, *, #72555, .T. ) ;
#52603=AXIS2_PLACEMENT_3D ( 'NONE', #140417, #6281, #115059 ) ;
#52604=ADVANCED_FACE ( 'NONE', ( #28433 ), #70547, .F. ) ;
#52605=CARTESIAN_POINT ( 'NONE',  ( 34.49999999999975131, -20.94567065516883630, 4.994342998332155226 ) ) ;
#52607=EDGE_LOOP ( 'NONE', ( #52830, #54180, #128717, #13059 ) ) ;
#52608=VERTEX_POINT ( 'NONE', #104543 ) ;
#52609=LINE ( 'NONE', #97537, #109221 ) ;
#52610=LINE ( 'NONE', #96104, #77693 ) ;
#52612=DIRECTION ( 'NONE',  ( -0.7071067811865486830, 0.7071067811865464625, 0.000000000000000000 ) ) ;
#52613=CARTESIAN_POINT ( 'NONE',  ( -45.18398860626900415, 28.73617430169818832, 5.000000000000000000 ) ) ;
#52616=DIRECTION ( 'NONE',  ( -0.7071067811865486830, -0.7071067811865464625, 0.000000000000000000 ) ) ;
#52617=CARTESIAN_POINT ( 'NONE',  ( -7.499999999999940492, -8.947814304570741228, 5.000000000000000000 ) ) ;
#52619=ORIENTED_EDGE ( 'NONE', *, *, #56437, .F. ) ;
#52620=CARTESIAN_POINT ( 'NONE',  ( 39.48921356237310221, -27.52281430457082934, 5.000000000000000000 ) ) ;
#52621=VERTEX_POINT ( 'NONE', #116852 ) ;
#52624=CARTESIAN_POINT ( 'NONE',  ( -26.27718569542921401, -21.72499999999999432, 5.000000000000000000 ) ) ;
#52625=VERTEX_POINT ( 'NONE', #14689 ) ;
#52626=CARTESIAN_POINT ( 'NONE',  ( -45.18398860626900415, 28.73617430169818832, 5.000000000000000000 ) ) ;
#52627=CARTESIAN_POINT ( 'NONE',  ( 0.000000000000000000, 0.000000000000000000, 5.000000000000000000 ) ) ;
#52630=CARTESIAN_POINT ( 'NONE',  ( 27.18398860626900060, 28.73617430169806042, 5.000000000000000000 ) ) ;
#52631=EDGE_CURVE ( 'NONE', #62501, #22625, #137911, .T. ) ;
#52633=VERTEX_POINT ( 'NONE', #105949 ) ;
#52635=CARTESIAN_POINT ( 'NONE',  ( 5.475998614145475507, 22.03583458319438648, 4.979811245910084061 ) ) ;
#52636=CARTESIAN_POINT ( 'NONE',  ( 23.54739889332687497, 7.099584588756134629, 5.000000000000000000 ) ) ;
#52638=DIRECTION ( 'NONE',  ( 0.7071067811865487940, 0.7071067811865463515, 0.000000000000000000 ) ) ;
#52639=VECTOR ( 'NONE', #2370, 1000.000000000000227 ) ;
#52642=ORIENTED_EDGE ( 'NONE', *, *, #108294, .F. ) ;
#52643=VECTOR ( 'NONE', #42872, 1000.000000000000000 ) ;
#52644=EDGE_CURVE ( 'NONE', #95429, #82756, #3764, .T. ) ;
#52646=ORIENTED_EDGE ( 'NONE', *, *, #84859, .T. ) ;
#52647=ADVANCED_FACE ( 'NONE', ( #127000 ), #59647, .F. ) ;
#52648=LINE ( 'NONE', #30182, #56907 ) ;
#52649=DIRECTION ( 'NONE',  ( -0.000000000000000000, 0.000000000000000000, 1.000000000000000000 ) ) ;
#52650=EDGE_CURVE ( 'NONE', #1167, #15218, #99285, .T. ) ;
#52651=CARTESIAN_POINT ( 'NONE',  ( 0.000000000000000000, 0.000000000000000000, 5.000000000000000000 ) ) ;
#52654=VERTEX_POINT ( 'NONE', #92960 ) ;
#52655=EDGE_CURVE ( 'NONE', #93595, #22044, #38584, .T. ) ;
#52656=LINE ( 'NONE', #119326, #26094 ) ;
#52657=DIRECTION ( 'NONE',  ( -0.7071067811865486830, -0.7071067811865464625, 0.000000000000000000 ) ) ;
#52658=ORIENTED_EDGE ( 'NONE', *, *, #59895, .F. ) ;
#52659=ADVANCED_FACE ( 'NONE', ( #137196 ), #37893, .F. ) ;
#52660=CARTESIAN_POINT ( 'NONE',  ( 39.29974487139159578, -27.71228299555233576, 4.000000000000000000 ) ) ;
#52661=DIRECTION ( 'NONE',  ( 0.7071067811865487940, 0.7071067811865463515, 0.000000000000000000 ) ) ;
#52662=DIRECTION ( 'NONE',  ( 0.6830127018922180770, -0.6830127018922204085, -0.2588190451025213501 ) ) ;
#52663=ORIENTED_EDGE ( 'NONE', *, *, #138615, .F. ) ;
#52665=EDGE_CURVE ( 'NONE', #53640, #25047, #105261, .T. ) ;
#52667=FACE_BOUND ( 'NONE', #119731, .T. ) ;
#52668=LINE ( 'NONE', #88174, #40938 ) ;
#52669=DIRECTION ( 'NONE',  ( 0.6830127018922180770, -0.6830127018922204085, -0.2588190451025213501 ) ) ;
#52670=DIRECTION ( 'NONE',  ( -0.7071067811865486830, 0.7071067811865464625, 0.000000000000000000 ) ) ;
#52671=AXIS2_PLACEMENT_3D ( 'NONE', #12606, #14755, #92297 ) ;
#52672=DIRECTION ( 'NONE',  ( 0.7071067811865486830, -0.7071067811865464625, -0.000000000000000000 ) ) ;
#52673=EDGE_CURVE ( 'NONE', #78369, #19810, #20370, .T. ) ;
#52674=CARTESIAN_POINT ( 'NONE',  ( -4.499999999999972466, 18.43112307739199451, 4.000000000000000000 ) ) ;
#52675=ORIENTED_EDGE ( 'NONE', *, *, #106127, .T. ) ;
#52676=CIRCLE ( 'NONE', #124397, 0.5000000000000004441 ) ;
#52677=ORIENTED_EDGE ( 'NONE', *, *, #100955, .F. ) ;
#52679=VERTEX_POINT ( 'NONE', #129150 ) ;
#52682=CARTESIAN_POINT ( 'NONE',  ( 34.92499999999998295, -13.91861162105995753, 18.69616556237237504 ) ) ;
#52683=CARTESIAN_POINT ( 'NONE',  ( 60.48921356237309510, -27.52281430457097500, 5.000000000000000000 ) ) ;
#52684=ORIENTED_EDGE ( 'NONE', *, *, #5394, .F. ) ;
#52685=CARTESIAN_POINT ( 'NONE',  ( -32.56319896779150724, -12.74070752338415247, 9.898150129686451137 ) ) ;
#52686=DIRECTION ( 'NONE',  ( -0.6830127018922180770, -0.6830127018922204085, -0.2588190451025213501 ) ) ;
#52688=LINE ( 'NONE', #7003, #48489 ) ;
#52691=CARTESIAN_POINT ( 'NONE',  ( 36.18398860626899705, 28.73617430169812437, 5.000000000000000000 ) ) ;
#52693=ORIENTED_EDGE ( 'NONE', *, *, #106186, .T. ) ;
#52696=ORIENTED_EDGE ( 'NONE', *, *, #87561, .F. ) ;
#52697=ORIENTED_EDGE ( 'NONE', *, *, #78441, .T. ) ;
#52699=VERTEX_POINT ( 'NONE', #62487 ) ;
#52700=ORIENTED_EDGE ( 'NONE', *, *, #75296, .T. ) ;
#52701=EDGE_CURVE ( 'NONE', #3406, #142587, #31982, .T. ) ;
#52702=CARTESIAN_POINT ( 'NONE',  ( 28.22674160717816960, -11.24070752338416490, 18.24660765846989108 ) ) ;
#52703=FACE_OUTER_BOUND ( 'NONE', #42407, .T. ) ;
#52704=VECTOR ( 'NONE', #104386, 1000.000000000000000 ) ;
#52706=CARTESIAN_POINT ( 'NONE',  ( -12.18398860626900060, 28.73617430169795739, 5.000000000000000000 ) ) ;
#52707=ADVANCED_FACE ( 'NONE', ( #142198 ), #18215, .F. ) ;
#52709=CARTESIAN_POINT ( 'NONE',  ( 7.499999999999944045, -9.462702396501008195, -9.474982329943534509 ) ) ;
#52710=CARTESIAN_POINT ( 'NONE',  ( 23.99999999999984013, -19.44781430457063465, 5.000000000000000000 ) ) ;
#52712=CARTESIAN_POINT ( 'NONE',  ( -20.99999999999985079, 17.96639925780207747, 5.000000000000000000 ) ) ;
#52713=EDGE_LOOP ( 'NONE', ( #100873, #45946, #9609, #75652 ) ) ;
#52714=DIRECTION ( 'NONE',  ( -0.000000000000000000, -0.000000000000000000, 1.000000000000000000 ) ) ;
#52715=EDGE_CURVE ( 'NONE', #8196, #126872, #63232, .T. ) ;
#52716=ORIENTED_EDGE ( 'NONE', *, *, #9230, .F. ) ;
#52717=ORIENTED_EDGE ( 'NONE', *, *, #111717, .F. ) ;
#52718=EDGE_LOOP ( 'NONE', ( #9688, #29944, #34732, #119963 ) ) ;
#52721=AXIS2_PLACEMENT_3D ( 'NONE', #99797, #133172, #469 ) ;
#52722=DIRECTION ( 'NONE',  ( 0.7071067811865486830, -0.7071067811865464625, -0.000000000000000000 ) ) ;
#52723=DIRECTION ( 'NONE',  ( -0.6830127018922180770, -0.6830127018922204085, -0.2588190451025213501 ) ) ;
#52725=EDGE_CURVE ( 'NONE', #18615, #58810, #7354, .T. ) ;
#52726=CARTESIAN_POINT ( 'NONE',  ( -2.999999999999975131, 5.587461875839191627, 4.000000000000000000 ) ) ;
#52727=ORIENTED_EDGE ( 'NONE', *, *, #101580, .F. ) ;
#52729=ORIENTED_EDGE ( 'NONE', *, *, #83462, .T. ) ;
#52731=AXIS2_PLACEMENT_3D ( 'NONE', #134933, #46515, #14545 ) ;
#52736=ORIENTED_EDGE ( 'NONE', *, *, #116301, .F. ) ;
#52738=ORIENTED_EDGE ( 'NONE', *, *, #115448, .T. ) ;
#52739=DIRECTION ( 'NONE',  ( -0.7071067811865486830, -0.7071067811865464625, 0.000000000000000000 ) ) ;
#52740=DIRECTION ( 'NONE',  ( 0.6830127018922180770, -0.6830127018922204085, -0.2588190451025213501 ) ) ;
#52741=LINE ( 'NONE', #86109, #112158 ) ;
#52742=PLANE ( 'NONE',  #99173 ) ;
#52743=LINE ( 'NONE', #84680, #85073 ) ;
#52744=DIRECTION ( 'NONE',  ( 0.7071067811865487940, 0.7071067811865463515, 0.000000000000000000 ) ) ;
#52745=ADVANCED_FACE ( 'NONE', ( #29828 ), #140731, .F. ) ;
#52747=DIRECTION ( 'NONE',  ( 0.6830127018922180770, -0.6830127018922204085, -0.2588190451025213501 ) ) ;
#52750=PLANE ( 'NONE',  #74288 ) ;
#52752=ORIENTED_EDGE ( 'NONE', *, *, #89164, .F. ) ;
#52755=EDGE_LOOP ( 'NONE', ( #137439, #6906, #87980, #143497 ) ) ;
#52756=EDGE_CURVE ( 'NONE', #76898, #136430, #85635, .T. ) ;
#52757=DIRECTION ( 'NONE',  ( 0.7071067811865486830, -0.7071067811865464625, -0.000000000000000000 ) ) ;
#52758=ORIENTED_EDGE ( 'NONE', *, *, #64465, .F. ) ;
#52759=PLANE ( 'NONE',  #69326 ) ;
#52760=VECTOR ( 'NONE', #86955, 1000.000000000000227 ) ;
#52761=ORIENTED_EDGE ( 'NONE', *, *, #133863, .T. ) ;
#52762=CARTESIAN_POINT ( 'NONE',  ( -17.20710678118642178, 15.75929247661555976, 5.000000000000000000 ) ) ;
#52763=EDGE_LOOP ( 'NONE', ( #42651, #24739, #40559, #68721, #90818 ) ) ;
#52766=DIRECTION ( 'NONE',  ( 0.6830127018922180770, -0.6830127018922204085, -0.2588190451025213501 ) ) ;
#52767=LINE ( 'NONE', #20857, #76376 ) ;
#52768=CARTESIAN_POINT ( 'NONE',  ( 78.18398860626899705, 28.73617430169841924, 5.000000000000000000 ) ) ;
#52770=DIRECTION ( 'NONE',  ( -0.3543493200069162685, -0.000000000000000000, -0.9351131265310288487 ) ) ;
#52776=EDGE_CURVE ( 'NONE', #74522, #84400, #87084, .T. ) ;
#52778=VERTEX_POINT ( 'NONE', #108080 ) ;
#52779=CARTESIAN_POINT ( 'NONE',  ( -17.99999999999987210, -8.731860332648849976, -2.120594902707582108 ) ) ;
#52780=ORIENTED_EDGE ( 'NONE', *, *, #26235, .F. ) ;
#52781=DIRECTION ( 'NONE',  ( -0.7071067811865486830, 0.7071067811865464625, 0.000000000000000000 ) ) ;
#52783=DIRECTION ( 'NONE',  ( -0.000000000000000000, 0.3543493200069153248, 0.9351131265310292928 ) ) ;
#52786=DIRECTION ( 'NONE',  ( -0.7071067811865487940, 0.7071067811865463515, -0.000000000000000000 ) ) ;
#52788=DIRECTION ( 'NONE',  ( -0.000000000000000000, 0.000000000000000000, 1.000000000000000000 ) ) ;
#52789=ORIENTED_EDGE ( 'NONE', *, *, #118915, .F. ) ;
#52792=CARTESIAN_POINT ( 'NONE',  ( 84.29974487139159578, -27.71228299555264840, 4.000000000000000000 ) ) ;
#52795=EDGE_LOOP ( 'NONE', ( #15410, #38424, #26263, #135073, #38387 ) ) ;
#52796=ORIENTED_EDGE ( 'NONE', *, *, #56857, .T. ) ;
#52797=VERTEX_POINT ( 'NONE', #141467 ) ;
#52798=EDGE_CURVE ( 'NONE', #38188, #46353, #74812, .T. ) ;
#52801=EDGE_CURVE ( 'NONE', #58810, #49145, #8747, .T. ) ;
#52803=EDGE_CURVE ( 'NONE', #95099, #136867, #76210, .T. ) ;
#52805=ORIENTED_EDGE ( 'NONE', *, *, #84750, .F. ) ;
#52806=EDGE_CURVE ( 'NONE', #18405, #83571, #42172, .T. ) ;
#52808=FACE_OUTER_BOUND ( 'NONE', #131106, .T. ) ;
#52810=ORIENTED_EDGE ( 'NONE', *, *, #61812, .T. ) ;
#52811=LINE ( 'NONE', #8565, #9468 ) ;
#52812=CARTESIAN_POINT ( 'NONE',  ( 18.29974487139159223, -27.71228299555219010, 4.000000000000000000 ) ) ;
#52813=CARTESIAN_POINT ( 'NONE',  ( 3.183988606268992161, 28.73617430169789699, 5.000000000000000000 ) ) ;
#52814=LINE ( 'NONE', #8569, #6840 ) ;
#52817=VECTOR ( 'NONE', #73559, 1000.000000000000000 ) ;
#52819=ORIENTED_EDGE ( 'NONE', *, *, #38986, .F. ) ;
#52820=CARTESIAN_POINT ( 'NONE',  ( -23.70025512860841133, -27.71228299555189523, 4.000000000000000000 ) ) ;
#52821=ADVANCED_FACE ( 'NONE', ( #41776 ), #77291, .F. ) ;
#52822=LINE ( 'NONE', #120950, #50160 ) ;
#52824=VECTOR ( 'NONE', #19014, 1000.000000000000000 ) ;
#52825=VECTOR ( 'NONE', #49167, 1000.000000000000114 ) ;
#52826=DIRECTION ( 'NONE',  ( 0.3543493200069162685, -0.000000000000000000, -0.9351131265310288487 ) ) ;
#52827=EDGE_CURVE ( 'NONE', #6574, #85157, #19304, .T. ) ;
#52829=ORIENTED_EDGE ( 'NONE', *, *, #137133, .T. ) ;
#52830=ORIENTED_EDGE ( 'NONE', *, *, #56498, .F. ) ;
#52831=CARTESIAN_POINT ( 'NONE',  ( 36.47336096364193736, -5.240707523384221744, 16.25846745537504034 ) ) ;
#52832=EDGE_LOOP ( 'NONE', ( #16384, #117866, #102042, #127253 ) ) ;
#52833=ORIENTED_EDGE ( 'NONE', *, *, #28110, .T. ) ;
#52837=LINE ( 'NONE', #32552, #77532 ) ;
#52838=VERTEX_POINT ( 'NONE', #54114 ) ;
#52839=DIRECTION ( 'NONE',  ( -0.7071067811865486830, -0.7071067811865464625, -0.000000000000000000 ) ) ;
#52841=DIRECTION ( 'NONE',  ( 0.6830127018922180770, -0.6830127018922204085, -0.2588190451025213501 ) ) ;
#52842=EDGE_CURVE ( 'NONE', #140745, #117806, #63560, .T. ) ;
#52843=CARTESIAN_POINT ( 'NONE',  ( 21.43680103220816591, -12.74070752338415247, 9.898150129686325016 ) ) ;
#52844=ORIENTED_EDGE ( 'NONE', *, *, #67548, .F. ) ;
#52848=ORIENTED_EDGE ( 'NONE', *, *, #95616, .F. ) ;
#52850=DIRECTION ( 'NONE',  ( 0.7071067811865487940, 0.7071067811865463515, -0.000000000000000000 ) ) ;
#52852=FACE_OUTER_BOUND ( 'NONE', #54849, .T. ) ;
#52854=CARTESIAN_POINT ( 'NONE',  ( 32.99999999999976552, -18.41253812416056945, 4.000000000000000000 ) ) ;
#52855=EDGE_LOOP ( 'NONE', ( #96053, #122600, #72149, #111706 ) ) ;
#52857=VERTEX_POINT ( 'NONE', #130223 ) ;
#52858=ADVANCED_FACE ( 'NONE', ( #98987 ), #132386, .T. ) ;
#52860=CARTESIAN_POINT ( 'NONE',  ( 1.171830600776465392, 0.7592924766157086447, 4.000000000000000000 ) ) ;
#52861=CARTESIAN_POINT ( 'NONE',  ( 34.92499999999998295, 8.947904407527573767, 10.03118784388415463 ) ) ;
#52863=DIRECTION ( 'NONE',  ( -0.7071067811865486830, 0.7071067811865464625, 0.000000000000000000 ) ) ;
#52864=DIRECTION ( 'NONE',  ( -0.000000000000000000, -0.3543493200069152693, 0.9351131265310292928 ) ) ;
#52865=DIRECTION ( 'NONE',  ( 0.6830127018922181881, 0.6830127018922202975, -0.2588190451025214056 ) ) ;
#52866=VECTOR ( 'NONE', #85496, 1000.000000000000000 ) ;
#52867=CARTESIAN_POINT ( 'NONE',  ( -11.99451991528749417, 28.92564299267946382, 4.000000000000000000 ) ) ;
#52868=FACE_OUTER_BOUND ( 'NONE', #99802, .T. ) ;
#52869=CARTESIAN_POINT ( 'NONE',  ( 29.99999999999980460, -3.412538124160717778, 4.000000000000000000 ) ) ;
#52870=LINE ( 'NONE', #97065, #93377 ) ;
#52871=EDGE_CURVE ( 'NONE', #69590, #60184, #118606, .T. ) ;
#52872=ORIENTED_EDGE ( 'NONE', *, *, #42876, .F. ) ;
#52873=ORIENTED_EDGE ( 'NONE', *, *, #20016, .F. ) ;
#52874=ORIENTED_EDGE ( 'NONE', *, *, #55806, .F. ) ;
#52875=ORIENTED_EDGE ( 'NONE', *, *, #67119, .F. ) ;
#52877=ORIENTED_EDGE ( 'NONE', *, *, #43677, .T. ) ;
#52879=DIRECTION ( 'NONE',  ( -0.6830127018922181881, 0.6830127018922202975, -0.2588190451025214056 ) ) ;
#52880=LINE ( 'NONE', #86967, #62020 ) ;
#52882=LINE ( 'NONE', #97850, #36986 ) ;
#52883=ORIENTED_EDGE ( 'NONE', *, *, #48234, .F. ) ;
#52884=CARTESIAN_POINT ( 'NONE',  ( 53.99451991528749062, 28.92564299267975869, 4.000000000000000000 ) ) ;
#52885=ORIENTED_EDGE ( 'NONE', *, *, #52482, .T. ) ;
#52886=CARTESIAN_POINT ( 'NONE',  ( 11.99999999999991296, -13.39766691384881803, -10.96608748226468677 ) ) ;
#52888=VERTEX_POINT ( 'NONE', #109162 ) ;
#52890=CARTESIAN_POINT ( 'NONE',  ( -21.18398860626899349, 28.73617430169802134, 5.000000000000000000 ) ) ;
#52891=PLANE ( 'NONE',  #9660 ) ;
#52892=CARTESIAN_POINT ( 'NONE',  ( 10.82816939922345156, 21.75929247661549581, 4.000000000000000000 ) ) ;
#52893=ORIENTED_EDGE ( 'NONE', *, *, #236, .T. ) ;
#52894=ORIENTED_EDGE ( 'NONE', *, *, #115466, .T. ) ;
#52895=PLANE ( 'NONE',  #125935 ) ;
#52896=VERTEX_POINT ( 'NONE', #19996 ) ;
#52897=DIRECTION ( 'NONE',  ( -0.3543493200069162685, -0.000000000000000000, -0.9351131265310288487 ) ) ;
#52899=CARTESIAN_POINT ( 'NONE',  ( -34.47516574401891631, -13.50948238788424938, 4.998110765256835286 ) ) ;
#52900=LINE ( 'NONE', #65267, #93520 ) ;
#52902=PLANE ( 'NONE',  #83160 ) ;
#52903=VECTOR ( 'NONE', #6518, 1000.000000000000227 ) ;
#52904=EDGE_CURVE ( 'NONE', #20428, #62928, #64242, .T. ) ;
#52906=EDGE_CURVE ( 'NONE', #79378, #85671, #65714, .T. ) ;
#52907=LINE ( 'NONE', #29736, #132516 ) ;
#52910=VECTOR ( 'NONE', #21672, 1000.000000000000000 ) ;
#52911=VECTOR ( 'NONE', #98406, 999.9999999999998863 ) ;
#52912=VECTOR ( 'NONE', #139191, 1000.000000000000227 ) ;
#52913=PLANE ( 'NONE',  #61041 ) ;
#52914=ORIENTED_EDGE ( 'NONE', *, *, #83986, .T. ) ;
#52915=VECTOR ( 'NONE', #126327, 1000.000000000000227 ) ;
#52916=ADVANCED_FACE ( 'NONE', ( #42514 ), #31615, .F. ) ;
#52918=ORIENTED_EDGE ( 'NONE', *, *, #57658, .T. ) ;
#52919=EDGE_LOOP ( 'NONE', ( #103500, #39234, #8859, #142174 ) ) ;
#52920=EDGE_CURVE ( 'NONE', #31963, #141805, #110564, .T. ) ;
#52921=CARTESIAN_POINT ( 'NONE',  ( -18.18398860626898994, 28.73617430169800002, 5.000000000000000000 ) ) ;
#52922=DIRECTION ( 'NONE',  ( 0.6830127018922180770, -0.6830127018922204085, -0.2588190451025213501 ) ) ;
#52923=VECTOR ( 'NONE', #137786, 1000.000000000000000 ) ;
#52924=ORIENTED_EDGE ( 'NONE', *, *, #120053, .F. ) ;
#52925=CARTESIAN_POINT ( 'NONE',  ( -7.499999999999944045, 19.46639925780207392, 5.000000000000000000 ) ) ;
#52926=VECTOR ( 'NONE', #61890, 999.9999999999998863 ) ;
#52927=CARTESIAN_POINT ( 'NONE',  ( -19.49999999999985789, -7.420205493532915142, -2.617629953481298788 ) ) ;
#52928=CARTESIAN_POINT ( 'NONE',  ( -24.46160355370555806, -9.740707523384173783, 17.74957260769605227 ) ) ;
#52930=LINE ( 'NONE', #97131, #115542 ) ;
#52931=DIRECTION ( 'NONE',  ( 0.3543493200069163795, -9.265275131829747941E-33, -0.9351131265310288487 ) ) ;
#52933=DIRECTION ( 'NONE',  ( -1.000000000000000000, -3.560121055573109579E-15, 0.000000000000000000 ) ) ;
#52935=DIRECTION ( 'NONE',  ( -0.6830127018922180770, -0.6830127018922204085, -0.2588190451025213501 ) ) ;
#52936=CARTESIAN_POINT ( 'NONE',  ( 0.4892135623730947680, -27.52281430457055578, 5.000000000000000000 ) ) ;
#52937=VECTOR ( 'NONE', #76883, 1000.000000000000000 ) ;
#52938=DIRECTION ( 'NONE',  ( 0.7071067811865487940, -0.7071067811865463515, 0.000000000000000000 ) ) ;
#52939=CARTESIAN_POINT ( 'NONE',  ( 54.29974487139159578, -27.71228299555243879, 4.000000000000000000 ) ) ;
#52940=DIRECTION ( 'NONE',  ( -0.7071067811865486830, -0.7071067811865464625, -0.000000000000000000 ) ) ;
#52941=ORIENTED_EDGE ( 'NONE', *, *, #34237, .T. ) ;
#52942=EDGE_CURVE ( 'NONE', #23280, #2318, #88867, .T. ) ;
#52943=( BOUNDED_CURVE ( )  B_SPLINE_CURVE ( 3, ( #141431, #68891, #2136, #34112 ),
 .UNSPECIFIED., .F., .F. ) 
 B_SPLINE_CURVE_WITH_KNOTS ( ( 4, 4 ),
 ( 2.356194490192346613, 2.506762762968578695 ),
 .UNSPECIFIED. ) 
 CURVE ( )  GEOMETRIC_REPRESENTATION_ITEM ( )  RATIONAL_B_SPLINE_CURVE ( ( 1.000000000000000000, 0.9981116584018945304, 0.9981116584018945304, 1.000000000000000000 ) ) 
 REPRESENTATION_ITEM ( '' )  );
#52945=ORIENTED_EDGE ( 'NONE', *, *, #105650, .F. ) ;
#52947=AXIS2_PLACEMENT_3D ( 'NONE', #82408, #18529, #103408 ) ;
#52948=ORIENTED_EDGE ( 'NONE', *, *, #56043, .F. ) ;
#52949=ORIENTED_EDGE ( 'NONE', *, *, #58748, .F. ) ;
#52950=EDGE_LOOP ( 'NONE', ( #66363, #1716, #74333, #24895 ) ) ;
#52951=LINE ( 'NONE', #120330, #61836 ) ;
#52953=CARTESIAN_POINT ( 'NONE',  ( 8.292893218813400580, 8.259292476615630818, 5.000000000000000000 ) ) ;
#52954=ORIENTED_EDGE ( 'NONE', *, *, #52586, .F. ) ;
#52957=DIRECTION ( 'NONE',  ( -0.7071067811865486830, -0.7071067811865464625, 0.000000000000000000 ) ) ;
#52959=LINE ( 'NONE', #30533, #115875 ) ;
#52960=VECTOR ( 'NONE', #83837, 999.9999999999998863 ) ;
#52964=ORIENTED_EDGE ( 'NONE', *, *, #9230, .T. ) ;
#52966=CARTESIAN_POINT ( 'NONE',  ( 27.18398860626900060, 28.73617430169806042, 5.000000000000000000 ) ) ;
#52967=CARTESIAN_POINT ( 'NONE',  ( -23.67183060077630685, -12.74070752338414891, 4.000000000000000000 ) ) ;
#52968=VECTOR ( 'NONE', #110704, 1000.000000000000000 ) ;
#52970=LINE ( 'NONE', #106626, #26114 ) ;
#52972=VECTOR ( 'NONE', #94942, 1000.000000000000000 ) ;
#52975=VERTEX_POINT ( 'NONE', #10542 ) ;
#52977=ADVANCED_FACE ( 'NONE', ( #54804 ), #88143, .T. ) ;
#52979=ORIENTED_EDGE ( 'NONE', *, *, #110348, .T. ) ;
#52983=VECTOR ( 'NONE', #95182, 1000.000000000000000 ) ;
#52985=DIRECTION ( 'NONE',  ( -0.3543493200069163240, 0.000000000000000000, 0.9351131265310288487 ) ) ;
#52986=ADVANCED_FACE ( 'NONE', ( #122161 ), #1092, .F. ) ;
#52989=DIRECTION ( 'NONE',  ( 0.3543493200069162685, -0.000000000000000000, -0.9351131265310288487 ) ) ;
#52991=ORIENTED_EDGE ( 'NONE', *, *, #58721, .T. ) ;
#52992=PLANE ( 'NONE',  #22414 ) ;
#52994=CARTESIAN_POINT ( 'NONE',  ( -21.18398860626899349, 28.73617430169802134, 5.000000000000000000 ) ) ;
#52995=LINE ( 'NONE', #66062, #64048 ) ;
#52997=DIRECTION ( 'NONE',  ( 0.7071067811865486830, -0.7071067811865464625, -0.000000000000000000 ) ) ;
#52998=ORIENTED_EDGE ( 'NONE', *, *, #26100, .T. ) ;
#53000=EDGE_CURVE ( 'NONE', #103666, #118878, #11979, .T. ) ;
#53001=EDGE_LOOP ( 'NONE', ( #22487, #50750, #115854, #51069 ) ) ;
#53002=DIRECTION ( 'NONE',  ( -0.000000000000000000, 0.000000000000000000, 1.000000000000000000 ) ) ;
#53003=EDGE_CURVE ( 'NONE', #55692, #46933, #69248, .T. ) ;
#53004=CARTESIAN_POINT ( 'NONE',  ( -27.18398860626900060, 28.73617430169806042, 5.000000000000000000 ) ) ;
#53005=DIRECTION ( 'NONE',  ( -0.000000000000000000, -0.3543493200069152693, 0.9351131265310292928 ) ) ;
#53006=LINE ( 'NONE', #88526, #50765 ) ;
#53007=EDGE_CURVE ( 'NONE', #16785, #97786, #123644, .T. ) ;
#53009=ORIENTED_EDGE ( 'NONE', *, *, #41833, .F. ) ;
#53010=CARTESIAN_POINT ( 'NONE',  ( -78.18398860626899705, 28.73617430169841924, 5.000000000000000000 ) ) ;
#53011=ORIENTED_EDGE ( 'NONE', *, *, #63569, .F. ) ;
#53012=ORIENTED_EDGE ( 'NONE', *, *, #59004, .F. ) ;
#53013=EDGE_CURVE ( 'NONE', #51392, #70680, #103270, .T. ) ;
#53014=ORIENTED_EDGE ( 'NONE', *, *, #65616, .F. ) ;
#53015=VECTOR ( 'NONE', #43490, 1000.000000000000227 ) ;
#53018=DIRECTION ( 'NONE',  ( -0.7071067811865486830, -0.7071067811865464625, 0.000000000000000000 ) ) ;
#53019=LINE ( 'NONE', #117553, #80368 ) ;
#53020=EDGE_CURVE ( 'NONE', #132991, #122347, #46081, .T. ) ;
#53021=CARTESIAN_POINT ( 'NONE',  ( -11.72174548431420149, 8.259292476615637923, 11.78515199841147520 ) ) ;
#53022=VECTOR ( 'NONE', #85861, 1000.000000000000227 ) ;
#53023=VECTOR ( 'NONE', #91406, 1000.000000000000000 ) ;
#53024=VECTOR ( 'NONE', #51790, 999.9999999999998863 ) ;
#53025=DIRECTION ( 'NONE',  ( -0.6830127018922181881, 0.6830127018922202975, -0.2588190451025214056 ) ) ;
#53026=VECTOR ( 'NONE', #7183, 1000.000000000000000 ) ;
#53027=FACE_BOUND ( 'NONE', #96730, .T. ) ;
#53028=VERTEX_POINT ( 'NONE', #77982 ) ;
#53029=PLANE ( 'NONE',  #2729 ) ;
#53030=PLANE ( 'NONE',  #11531 ) ;
#53032=CARTESIAN_POINT ( 'NONE',  ( 21.18398860626899349, 28.73617430169802134, 5.000000000000000000 ) ) ;
#53034=ADVANCED_FACE ( 'NONE', ( #111289 ), #45376, .F. ) ;
#53035=VERTEX_POINT ( 'NONE', #14119 ) ;
#53036=VECTOR ( 'NONE', #76887, 1000.000000000000227 ) ;
#53037=DIRECTION ( 'NONE',  ( -0.7071067811865486830, -0.7071067811865464625, 0.000000000000000000 ) ) ;
#53038=ORIENTED_EDGE ( 'NONE', *, *, #49505, .F. ) ;
#53039=ADVANCED_FACE ( 'NONE', ( #68543 ), #56960, .F. ) ;
#53041=ORIENTED_EDGE ( 'NONE', *, *, #67312, .T. ) ;
#53042=DIRECTION ( 'NONE',  ( -0.000000000000000000, 1.000000000000000000, -0.000000000000000000 ) ) ;
#53043=DIRECTION ( 'NONE',  ( 0.7071067811865486830, -0.7071067811865464625, -0.000000000000000000 ) ) ;
#53044=ORIENTED_EDGE ( 'NONE', *, *, #49078, .F. ) ;
#53045=DIRECTION ( 'NONE',  ( -0.000000000000000000, -0.3543493200069152693, 0.9351131265310292928 ) ) ;
#53046=VECTOR ( 'NONE', #47661, 1000.000000000000000 ) ;
#53047=VECTOR ( 'NONE', #45192, 999.9999999999998863 ) ;
#53048=VECTOR ( 'NONE', #40869, 1000.000000000000000 ) ;
#53049=DIRECTION ( 'NONE',  ( -0.7071067811865487940, 0.7071067811865463515, 0.000000000000000000 ) ) ;
#53050=DIRECTION ( 'NONE',  ( 1.000000000000000000, -0.000000000000000000, 0.000000000000000000 ) ) ;
#53051=CARTESIAN_POINT ( 'NONE',  ( 0.000000000000000000, -21.72500000000000142, 4.500000000000000888 ) ) ;
#53052=PLANE ( 'NONE',  #42502 ) ;
#53053=CARTESIAN_POINT ( 'NONE',  ( 34.42499999999998295, 21.72500000000000142, 0.4999999999999995559 ) ) ;
#53054=ORIENTED_EDGE ( 'NONE', *, *, #61812, .F. ) ;
#53055=EDGE_LOOP ( 'NONE', ( #72458, #28490, #103680, #20654 ) ) ;
#53056=VECTOR ( 'NONE', #112734, 999.9999999999998863 ) ;
#53057=FACE_OUTER_BOUND ( 'NONE', #123228, .T. ) ;
#53058=FACE_OUTER_BOUND ( 'NONE', #110253, .T. ) ;
#53059=VERTEX_POINT ( 'NONE', #91010 ) ;
#53060=ORIENTED_EDGE ( 'NONE', *, *, #107533, .F. ) ;
#53061=AXIS2_PLACEMENT_3D ( 'NONE', #108357, #117818, #18506 ) ;
#53062=ORIENTED_EDGE ( 'NONE', *, *, #50133, .T. ) ;
#53063=LINE ( 'NONE', #131360, #74512 ) ;
#53064=CARTESIAN_POINT ( 'NONE',  ( -25.17183060077629975, 12.75929247661559174, 4.000000000000000000 ) ) ;
#53065=CARTESIAN_POINT ( 'NONE',  ( 48.18398860626899705, 28.73617430169820608, 5.000000000000000000 ) ) ;
#53066=EDGE_LOOP ( 'NONE', ( #85846, #90043, #4869, #92282 ) ) ;
#53067=VECTOR ( 'NONE', #76546, 1000.000000000000000 ) ;
#53068=DIRECTION ( 'NONE',  ( 0.7071067811865487940, 0.7071067811865463515, 0.000000000000000000 ) ) ;
#53070=LINE ( 'NONE', #66830, #426 ) ;
#53073=VERTEX_POINT ( 'NONE', #134505 ) ;
#53075=PLANE ( 'NONE',  #106722 ) ;
#53076=EDGE_CURVE ( 'NONE', #130333, #109240, #89550, .T. ) ;
#53077=LINE ( 'NONE', #98038, #19430 ) ;
#53078=FACE_OUTER_BOUND ( 'NONE', #40680, .T. ) ;
#53079=VERTEX_POINT ( 'NONE', #102593 ) ;
#53081=VERTEX_POINT ( 'NONE', #47531 ) ;
#53082=CARTESIAN_POINT ( 'NONE',  ( -72.18398860626899705, 28.73617430169837661, 5.000000000000000000 ) ) ;
#53084=DIRECTION ( 'NONE',  ( 0.7071067811865486830, -0.7071067811865464625, -0.000000000000000000 ) ) ;
#53085=VERTEX_POINT ( 'NONE', #91691 ) ;
#53086=EDGE_CURVE ( 'NONE', #111174, #64090, #135916, .T. ) ;
#53089=ORIENTED_EDGE ( 'NONE', *, *, #133532, .F. ) ;
#53090=LINE ( 'NONE', #99444, #2200 ) ;
#53091=CARTESIAN_POINT ( 'NONE',  ( -3.005480084712505828, 28.92564299267936079, 4.000000000000000000 ) ) ;
#53092=ORIENTED_EDGE ( 'NONE', *, *, #64744, .F. ) ;
#53094=DIRECTION ( 'NONE',  ( 0.6830127018922181881, 0.6830127018922202975, -0.2588190451025214056 ) ) ;
#53096=ORIENTED_EDGE ( 'NONE', *, *, #62026, .F. ) ;
#53098=EDGE_CURVE ( 'NONE', #130142, #139208, #13393, .T. ) ;
#53099=ORIENTED_EDGE ( 'NONE', *, *, #84317, .T. ) ;
#53101=DIRECTION ( 'NONE',  ( -0.000000000000000000, 0.3543493200069153248, 0.9351131265310292928 ) ) ;
#53102=ADVANCED_FACE ( 'NONE', ( #23580 ), #112037, .F. ) ;
#53107=ORIENTED_EDGE ( 'NONE', *, *, #6623, .T. ) ;
#53108=EDGE_CURVE ( 'NONE', #17366, #18293, #79448, .T. ) ;
#53110=CARTESIAN_POINT ( 'NONE',  ( -84.18398860626899705, 28.73617430169846187, 5.000000000000000000 ) ) ;
#53112=CARTESIAN_POINT ( 'NONE',  ( -17.81601139373099940, 28.73617430169775133, 5.000000000000000000 ) ) ;
#53114=CARTESIAN_POINT ( 'NONE',  ( -21.78162688292479388, 21.74787736706805674, 4.999607392498049308 ) ) ;
#53115=EDGE_CURVE ( 'NONE', #21869, #127158, #29285, .T. ) ;
#53116=EDGE_LOOP ( 'NONE', ( #102474, #92107, #94062, #80866, #98508 ) ) ;
#53117=LINE ( 'NONE', #74186, #16316 ) ;
#53118=ORIENTED_EDGE ( 'NONE', *, *, #92692, .T. ) ;
#53119=ORIENTED_EDGE ( 'NONE', *, *, #2997, .F. ) ;
#53120=AXIS2_PLACEMENT_3D ( 'NONE', #95461, #84607, #73715 ) ;
#53121=DIRECTION ( 'NONE',  ( -0.3543493200069163240, -0.000000000000000000, -0.9351131265310288487 ) ) ;
#53122=DIRECTION ( 'NONE',  ( -0.000000000000000000, 0.3543493200069153248, 0.9351131265310292928 ) ) ;
#53124=EDGE_CURVE ( 'NONE', #4075, #87580, #93833, .T. ) ;
#53126=ORIENTED_EDGE ( 'NONE', *, *, #139102, .T. ) ;
#53128=DIRECTION ( 'NONE',  ( 0.7071067811865487940, 0.7071067811865463515, 0.000000000000000000 ) ) ;
#53129=VECTOR ( 'NONE', #125092, 1000.000000000000000 ) ;
#53130=CARTESIAN_POINT ( 'NONE',  ( -8.526639036357797963, -5.240707523384225297, 16.25846745537493732 ) ) ;
#53131=DIRECTION ( 'NONE',  ( -0.7071067811865486830, 0.7071067811865464625, 0.000000000000000000 ) ) ;
#53132=LINE ( 'NONE', #8185, #24582 ) ;
#53133=ORIENTED_EDGE ( 'NONE', *, *, #113226, .F. ) ;
#53134=CARTESIAN_POINT ( 'NONE',  ( -12.81246187583938401, -22.22500000000000142, 4.000000000000000000 ) ) ;
#53135=CARTESIAN_POINT ( 'NONE',  ( 19.27928215921719612, -2.789594763390444321, 4.000000000000000000 ) ) ;
#53136=EDGE_CURVE ( 'NONE', #106976, #50763, #138061, .T. ) ;
#53139=CARTESIAN_POINT ( 'NONE',  ( 2.994519915287485734, 28.92564299267940342, 4.000000000000000000 ) ) ;
#53140=CARTESIAN_POINT ( 'NONE',  ( 69.48921356237309510, -27.52281430457103895, 5.000000000000000000 ) ) ;
#53142=DIRECTION ( 'NONE',  ( -0.6830127018922180770, -0.6830127018922204085, -0.2588190451025213501 ) ) ;
#53144=DIRECTION ( 'NONE',  ( 0.7071067811865487940, 0.7071067811865463515, 0.000000000000000000 ) ) ;
#53145=VECTOR ( 'NONE', #116231, 1000.000000000000000 ) ;
#53146=VERTEX_POINT ( 'NONE', #117009 ) ;
#53147=ORIENTED_EDGE ( 'NONE', *, *, #138670, .T. ) ;
#53149=CARTESIAN_POINT ( 'NONE',  ( -29.67183060077626422, -6.740707523384212863, 4.000000000000000000 ) ) ;
#53150=DIRECTION ( 'NONE',  ( -1.000000000000000000, 0.000000000000000000, -0.000000000000000000 ) ) ;
#53151=EDGE_CURVE ( 'NONE', #143140, #123173, #105409, .T. ) ;
#53152=VECTOR ( 'NONE', #25130, 1000.000000000000000 ) ;
#53153=PLANE ( 'NONE',  #32279 ) ;
#53154=ORIENTED_EDGE ( 'NONE', *, *, #82042, .T. ) ;
#53155=LINE ( 'NONE', #108954, #123221 ) ;
#53156=EDGE_CURVE ( 'NONE', #143522, #4786, #4611, .T. ) ;
#53157=EDGE_CURVE ( 'NONE', #129470, #111735, #73528, .T. ) ;
#53159=VERTEX_POINT ( 'NONE', #38746 ) ;
#53160=DIRECTION ( 'NONE',  ( 0.7071067811865486830, -0.7071067811865464625, -0.000000000000000000 ) ) ;
#53161=VERTEX_POINT ( 'NONE', #114843 ) ;
#53162=VERTEX_POINT ( 'NONE', #138789 ) ;
#53163=CARTESIAN_POINT ( 'NONE',  ( 11.99999999999990941, -13.06887692260767686, 4.000000000000000000 ) ) ;
#53165=VECTOR ( 'NONE', #7308, 1000.000000000000114 ) ;
#53166=EDGE_CURVE ( 'NONE', #52039, #121499, #48925, .T. ) ;
#53168=CARTESIAN_POINT ( 'NONE',  ( -10.49999999999993250, -14.70932175296478839, -11.46312253303834794 ) ) ;
#53169=VECTOR ( 'NONE', #141210, 1000.000000000000114 ) ;
#53170=DIRECTION ( 'NONE',  ( 0.7071067811865487940, 0.7071067811865463515, 0.000000000000000000 ) ) ;
#53171=EDGE_LOOP ( 'NONE', ( #37069, #21842, #119234, #29876 ) ) ;
#53172=EDGE_CURVE ( 'NONE', #62444, #9144, #139524, .T. ) ;
#53173=CARTESIAN_POINT ( 'NONE',  ( 5.999999999999974243, -19.44781430457062754, 5.000000000000000000 ) ) ;
#53176=ORIENTED_EDGE ( 'NONE', *, *, #2078, .F. ) ;
#53177=VECTOR ( 'NONE', #126061, 999.9999999999998863 ) ;
#53179=VECTOR ( 'NONE', #26975, 1000.000000000000227 ) ;
#53181=CARTESIAN_POINT ( 'NONE',  ( -8.994519915287490619, 28.92564299267944250, 4.000000000000000000 ) ) ;
#53182=DIRECTION ( 'NONE',  ( -0.7071067811865487940, 0.7071067811865463515, 0.000000000000000000 ) ) ;
#53183=AXIS2_PLACEMENT_3D ( 'NONE', #74955, #108948, #29974 ) ;
#53184=CARTESIAN_POINT ( 'NONE',  ( 56.99451991528749062, 28.92564299267978001, 4.000000000000000000 ) ) ;
#53185=ORIENTED_EDGE ( 'NONE', *, *, #53858, .F. ) ;
#53186=ADVANCED_FACE ( 'NONE', ( #28597 ), #125771, .F. ) ;
#53190=CARTESIAN_POINT ( 'NONE',  ( -24.69524342170288023, 1.235879655689124501, 4.000000000000000000 ) ) ;
#53192=ORIENTED_EDGE ( 'NONE', *, *, #85267, .F. ) ;
#53194=PLANE ( 'NONE',  #28369 ) ;
#53195=DIRECTION ( 'NONE',  ( 1.000000000000000000, 0.000000000000000000, 0.000000000000000000 ) ) ;
#53196=EDGE_CURVE ( 'NONE', #33900, #17266, #40208, .T. ) ;
#53198=ORIENTED_EDGE ( 'NONE', *, *, #28679, .T. ) ;
#53199=CARTESIAN_POINT ( 'NONE',  ( 9.981552653643248618, 18.75929247661552424, 20.33588619593440683 ) ) ;
#53200=ORIENTED_EDGE ( 'NONE', *, *, #88027, .F. ) ;
#53201=LINE ( 'NONE', #86577, #97827 ) ;
#53202=CARTESIAN_POINT ( 'NONE',  ( 39.48921356237310221, -27.52281430457082934, 5.000000000000000000 ) ) ;
#53204=FACE_OUTER_BOUND ( 'NONE', #35189, .T. ) ;
#53205=FACE_BOUND ( 'NONE', #50132, .T. ) ;
#53206=PLANE ( 'NONE',  #8482 ) ;
#53212=ORIENTED_EDGE ( 'NONE', *, *, #78359, .F. ) ;
#53213=EDGE_CURVE ( 'NONE', #115415, #88391, #116299, .T. ) ;
#53214=ORIENTED_EDGE ( 'NONE', *, *, #104179, .F. ) ;
#53216=ORIENTED_EDGE ( 'NONE', *, *, #113633, .T. ) ;
#53217=DIRECTION ( 'NONE',  ( 0.7071067811865487940, -0.7071067811865463515, 0.000000000000000000 ) ) ;
#53218=EDGE_LOOP ( 'NONE', ( #69987, #17926, #123850, #83739 ) ) ;
#53219=CARTESIAN_POINT ( 'NONE',  ( 3.183988606268992161, 28.73617430169789699, 5.000000000000000000 ) ) ;
#53221=DIRECTION ( 'NONE',  ( 0.3543493200069162685, -0.000000000000000000, -0.9351131265310288487 ) ) ;
#53222=AXIS2_PLACEMENT_3D ( 'NONE', #123734, #13484, #101957 ) ;
#53223=LINE ( 'NONE', #120611, #17616 ) ;
#53224=DIRECTION ( 'NONE',  ( 0.7071067811865487940, 0.7071067811865463515, 0.000000000000000000 ) ) ;
#53225=CARTESIAN_POINT ( 'NONE',  ( -24.79333936457829779, 21.75929247661549581, 4.998822639870701856 ) ) ;
#53226=CARTESIAN_POINT ( 'NONE',  ( -21.48921356237309155, -27.52281430457070499, 5.000000000000000000 ) ) ;
#53228=VERTEX_POINT ( 'NONE', #26444 ) ;
#53229=VECTOR ( 'NONE', #94265, 1000.000000000000000 ) ;
#53232=ORIENTED_EDGE ( 'NONE', *, *, #46304, .T. ) ;
#53233=DIRECTION ( 'NONE',  ( -0.7071067811865486830, -0.7071067811865464625, 0.000000000000000000 ) ) ;
#53234=FACE_OUTER_BOUND ( 'NONE', #93906, .T. ) ;
#53235=VECTOR ( 'NONE', #24889, 1000.000000000000227 ) ;
#53236=EDGE_LOOP ( 'NONE', ( #89570, #51222, #38446 ) ) ;
#53237=ORIENTED_EDGE ( 'NONE', *, *, #93878, .T. ) ;
#53238=ORIENTED_EDGE ( 'NONE', *, *, #110348, .F. ) ;
#53240=VERTEX_POINT ( 'NONE', #18380 ) ;
#53241=AXIS2_PLACEMENT_3D ( 'NONE', #61744, #18172, #116085 ) ;
#53242=DIRECTION ( 'NONE',  ( 0.7071067811865486830, -0.7071067811865464625, -0.000000000000000000 ) ) ;
#53245=VERTEX_POINT ( 'NONE', #137357 ) ;
#53246=CARTESIAN_POINT ( 'NONE',  ( -63.48921356237309510, -27.52281430457099631, 5.000000000000000000 ) ) ;
#53247=ORIENTED_EDGE ( 'NONE', *, *, #42945, .T. ) ;
#53249=VECTOR ( 'NONE', #61740, 1000.000000000000000 ) ;
#53250=AXIS2_PLACEMENT_3D ( 'NONE', #67263, #123798, #91175 ) ;
#53251=LINE ( 'NONE', #119915, #116914 ) ;
#53252=PLANE ( 'NONE',  #65626 ) ;
#53253=ORIENTED_EDGE ( 'NONE', *, *, #21019, .F. ) ;
#53255=PLANE ( 'NONE',  #16811 ) ;
#53256=FACE_OUTER_BOUND ( 'NONE', #70421, .T. ) ;
#53257=ORIENTED_EDGE ( 'NONE', *, *, #5215, .F. ) ;
#53258=VECTOR ( 'NONE', #46822, 1000.000000000000000 ) ;
#53259=CARTESIAN_POINT ( 'NONE',  ( -20.29289321881330821, -6.740707523384214639, 5.000000000000000000 ) ) ;
#53260=ORIENTED_EDGE ( 'NONE', *, *, #94378, .T. ) ;
#53261=ORIENTED_EDGE ( 'NONE', *, *, #68231, .T. ) ;
#53262=ORIENTED_EDGE ( 'NONE', *, *, #73143, .T. ) ;
#53264=DIRECTION ( 'NONE',  ( 0.7071067811865487940, -0.7071067811865463515, -0.000000000000000000 ) ) ;
#53266=VECTOR ( 'NONE', #108039, 1000.000000000000000 ) ;
#53267=CARTESIAN_POINT ( 'NONE',  ( -53.99451991528749062, 28.92564299267975869, 4.000000000000000000 ) ) ;
#53268=ADVANCED_FACE ( 'NONE', ( #127917 ), #92383, .F. ) ;
#53269=LINE ( 'NONE', #33004, #91074 ) ;
#53271=ADVANCED_FACE ( 'NONE', ( #106841 ), #136614, .F. ) ;
#53272=EDGE_CURVE ( 'NONE', #136399, #89877, #27861, .T. ) ;
#53274=VECTOR ( 'NONE', #83827, 1000.000000000000000 ) ;
#53276=VERTEX_POINT ( 'NONE', #16235 ) ;
#53277=VECTOR ( 'NONE', #50868, 1000.000000000000000 ) ;
#53278=DIRECTION ( 'NONE',  ( -0.7071067811865486830, -0.7071067811865464625, 0.000000000000000000 ) ) ;
#53279=EDGE_CURVE ( 'NONE', #27100, #138721, #104707, .T. ) ;
#53280=EDGE_CURVE ( 'NONE', #34606, #109090, #16995, .T. ) ;
#53281=DIRECTION ( 'NONE',  ( 0.7071067811865486830, -0.7071067811865464625, -0.000000000000000000 ) ) ;
#53282=ORIENTED_EDGE ( 'NONE', *, *, #107521, .T. ) ;
#53283=AXIS2_PLACEMENT_3D ( 'NONE', #93162, #60575, #125807 ) ;
#53284=CARTESIAN_POINT ( 'NONE',  ( -16.49999999999988276, 12.43112307739205313, 4.000000000000000000 ) ) ;
#53285=CARTESIAN_POINT ( 'NONE',  ( -34.42500000000001137, -19.45860074219779534, 5.000000000000000000 ) ) ;
#53286=ORIENTED_EDGE ( 'NONE', *, *, #96748, .T. ) ;
#53287=VERTEX_POINT ( 'NONE', #61267 ) ;
#53288=EDGE_CURVE ( 'NONE', #89845, #118518, #83713, .T. ) ;
#53289=CARTESIAN_POINT ( 'NONE',  ( -14.99451991528749595, 28.92564299267948513, 4.000000000000000000 ) ) ;
#53290=DIRECTION ( 'NONE',  ( -0.3543493200069162685, -0.000000000000000000, -0.9351131265310288487 ) ) ;
#53292=VECTOR ( 'NONE', #84219, 1000.000000000000000 ) ;
#53293=LINE ( 'NONE', #8332, #134940 ) ;
#53294=CARTESIAN_POINT ( 'NONE',  ( 57.18398860626899705, 28.73617430169827358, 5.000000000000000000 ) ) ;
#53295=CARTESIAN_POINT ( 'NONE',  ( 22.82900182742193351, 7.795401085224272109, 5.000000000000000000 ) ) ;
#53297=DIRECTION ( 'NONE',  ( -0.000000000000000000, 0.3543493200069153248, 0.9351131265310292928 ) ) ;
#53300=DIRECTION ( 'NONE',  ( -0.7071067811865487940, 0.7071067811865463515, 0.000000000000000000 ) ) ;
#53303=VERTEX_POINT ( 'NONE', #97374 ) ;
#53304=ORIENTED_EDGE ( 'NONE', *, *, #15070, .F. ) ;
#53305=AXIS2_PLACEMENT_3D ( 'NONE', #131537, #108310, #118505 ) ;
#53306=PLANE ( 'NONE',  #135810 ) ;
#53308=ORIENTED_EDGE ( 'NONE', *, *, #134826, .T. ) ;
#53309=CARTESIAN_POINT ( 'NONE',  ( 32.91508676806217437, -12.74070752338415957, 18.74364270924361975 ) ) ;
#53310=FACE_OUTER_BOUND ( 'NONE', #106450, .T. ) ;
#53311=EDGE_LOOP ( 'NONE', ( #36479, #13594, #30358, #135483 ) ) ;
#53312=PLANE ( 'NONE',  #136497 ) ;
#53313=CARTESIAN_POINT ( 'NONE',  ( 2.999999999999981792, -15.41253812416060143, 4.000000000000000000 ) ) ;
#53314=PLANE ( 'NONE',  #6026 ) ;
#53316=EDGE_LOOP ( 'NONE', ( #14687, #105839, #42546, #128339 ) ) ;
#53318=CARTESIAN_POINT ( 'NONE',  ( -23.99999999999982947, -8.731860332648864187, -2.120594902707593654 ) ) ;
#53319=EDGE_CURVE ( 'NONE', #49422, #105592, #131473, .T. ) ;
#53320=VECTOR ( 'NONE', #102560, 1000.000000000000000 ) ;
#53321=DIRECTION ( 'NONE',  ( -0.7071067811865486830, -0.7071067811865464625, -0.000000000000000000 ) ) ;
#53322=CARTESIAN_POINT ( 'NONE',  ( -24.18398860626899705, 28.73617430169804265, 5.000000000000000000 ) ) ;
#53324=PLANE ( 'NONE',  #16175 ) ;
#53325=DIRECTION ( 'NONE',  ( -0.7071067811865487940, 0.7071067811865463515, 0.000000000000000000 ) ) ;
#53326=ORIENTED_EDGE ( 'NONE', *, *, #90651, .F. ) ;
#53327=CARTESIAN_POINT ( 'NONE',  ( 19.49999999999987566, 19.46639925780206326, 5.000000000000000000 ) ) ;
#53328=CARTESIAN_POINT ( 'NONE',  ( 5.999999999999967137, 5.966399257802200040, 5.000000000000000000 ) ) ;
#53330=ADVANCED_FACE ( 'NONE', ( #19830 ), #142356, .F. ) ;
#53332=VECTOR ( 'NONE', #121575, 1000.000000000000000 ) ;
#53333=CARTESIAN_POINT ( 'NONE',  ( 4.499999999999970690, -15.29013452822854013, 0.3645803511610444803 ) ) ;
#53334=VECTOR ( 'NONE', #65927, 999.9999999999998863 ) ;
#53336=ORIENTED_EDGE ( 'NONE', *, *, #74906, .T. ) ;
#53337=VECTOR ( 'NONE', #56097, 1000.000000000000227 ) ;
#53340=DIRECTION ( 'NONE',  ( 0.7071067811865486830, -0.7071067811865464625, -0.000000000000000000 ) ) ;
#53341=FACE_OUTER_BOUND ( 'NONE', #61455, .T. ) ;
#53343=VECTOR ( 'NONE', #134057, 1000.000000000000000 ) ;
#53344=VECTOR ( 'NONE', #70128, 1000.000000000000227 ) ;
#53345=AXIS2_PLACEMENT_3D ( 'NONE', #99828, #101971, #57786 ) ;
#53347=PLANE ( 'NONE',  #7208 ) ;
#53348=EDGE_CURVE ( 'NONE', #141092, #43222, #52459, .T. ) ;
#53349=AXIS2_PLACEMENT_3D ( 'NONE', #7026, #108487, #97648 ) ;
#53350=CARTESIAN_POINT ( 'NONE',  ( 11.70025512860841133, -27.71228299555198049, 4.000000000000000000 ) ) ;
#53351=DIRECTION ( 'NONE',  ( -0.7071067811865487940, 0.7071067811865463515, -0.000000000000000000 ) ) ;
#53353=FACE_OUTER_BOUND ( 'NONE', #55456, .T. ) ;
#53354=ORIENTED_EDGE ( 'NONE', *, *, #56366, .F. ) ;
#53356=LINE ( 'NONE', #21455, #140304 ) ;
#53357=CARTESIAN_POINT ( 'NONE',  ( 33.79289321881321939, 6.759292476615653023, 5.000000000000000000 ) ) ;
#53358=VECTOR ( 'NONE', #89882, 1000.000000000000000 ) ;
#53359=EDGE_CURVE ( 'NONE', #95686, #122429, #65535, .T. ) ;
#53361=ORIENTED_EDGE ( 'NONE', *, *, #49910, .F. ) ;
#53364=EDGE_LOOP ( 'NONE', ( #3086, #45607, #6224, #63262 ) ) ;
#53365=EDGE_CURVE ( 'NONE', #141369, #51675, #42338, .T. ) ;
#53366=CARTESIAN_POINT ( 'NONE',  ( -9.134995737516172554, 3.759292476615678336, 15.36553568819728355 ) ) ;
#53367=CARTESIAN_POINT ( 'NONE',  ( 11.99999999999991296, -7.068876922607741697, 4.000000000000000000 ) ) ;
#53368=VECTOR ( 'NONE', #139078, 999.9999999999998863 ) ;
#53369=FACE_OUTER_BOUND ( 'NONE', #106537, .T. ) ;
#53370=LINE ( 'NONE', #9101, #38580 ) ;
#53371=EDGE_LOOP ( 'NONE', ( #26338, #85282, #59623, #87310 ) ) ;
#53372=CARTESIAN_POINT ( 'NONE',  ( 4.499999999999972466, 10.08746187583913922, 4.000000000000000000 ) ) ;
#53375=VECTOR ( 'NONE', #55345, 1000.000000000000000 ) ;
#53377=AXIS2_PLACEMENT_3D ( 'NONE', #128496, #17560, #16873 ) ;
#53378=DIRECTION ( 'NONE',  ( 0.7071067811865487940, 0.7071067811865463515, -0.000000000000000000 ) ) ;
#53379=VECTOR ( 'NONE', #67639, 999.9999999999998863 ) ;
#53380=LINE ( 'NONE', #97587, #105803 ) ;
#53381=CARTESIAN_POINT ( 'NONE',  ( -42.18398860626899705, 28.73617430169816700, 5.000000000000000000 ) ) ;
#53383=ORIENTED_EDGE ( 'NONE', *, *, #79749, .F. ) ;
#53384=ORIENTED_EDGE ( 'NONE', *, *, #12367, .T. ) ;
#53385=EDGE_CURVE ( 'NONE', #42960, #45983, #140204, .T. ) ;
#53386=FACE_BOUND ( 'NONE', #96237, .T. ) ;
#53387=VECTOR ( 'NONE', #30861, 1000.000000000000227 ) ;
#53388=DIRECTION ( 'NONE',  ( -0.7071067811865487940, 0.7071067811865463515, -0.000000000000000000 ) ) ;
#53389=EDGE_CURVE ( 'NONE', #140659, #13117, #132199, .T. ) ;
#53391=FACE_OUTER_BOUND ( 'NONE', #26260, .T. ) ;
#53392=CARTESIAN_POINT ( 'NONE',  ( -10.49999999999992895, 16.77039438581778796, 0.4657186855307983153 ) ) ;
#53395=EDGE_CURVE ( 'NONE', #102321, #137557, #130044, .T. ) ;
#53396=VECTOR ( 'NONE', #84537, 1000.000000000000000 ) ;
#53397=VERTEX_POINT ( 'NONE', #21975 ) ;
#53399=EDGE_LOOP ( 'NONE', ( #82352, #51217, #102971, #12507 ) ) ;
#53400=EDGE_CURVE ( 'NONE', #87047, #53796, #66224, .T. ) ;
#53403=DIRECTION ( 'NONE',  ( -0.000000000000000000, 0.3543493200069153248, 0.9351131265310292928 ) ) ;
#53404=EDGE_CURVE ( 'NONE', #127403, #19828, #130780, .T. ) ;
#53405=DIRECTION ( 'NONE',  ( -8.817971600062198362E-18, -0.3543493200069152693, 0.9351131265310292928 ) ) ;
#53406=CARTESIAN_POINT ( 'NONE',  ( -21.18398860626899349, 28.73617430169802134, 5.000000000000000000 ) ) ;
#53407=EDGE_CURVE ( 'NONE', #103883, #33542, #110397, .T. ) ;
#53408=ORIENTED_EDGE ( 'NONE', *, *, #93759, .T. ) ;
#53409=LINE ( 'NONE', #130991, #103818 ) ;
#53410=CARTESIAN_POINT ( 'NONE',  ( -33.29974487139158867, -27.71228299555229313, 4.000000000000000000 ) ) ;
#53411=CARTESIAN_POINT ( 'NONE',  ( 26.27718569542921401, -21.72499999999999432, 5.000000000000000000 ) ) ;
#53412=LINE ( 'NONE', #109219, #27685 ) ;
#53415=ORIENTED_EDGE ( 'NONE', *, *, #10969, .T. ) ;
#53416=PLANE ( 'NONE',  #70477 ) ;
#53419=CARTESIAN_POINT ( 'NONE',  ( -34.92500000000001137, 20.81665438641021382, 4.500000000000000888 ) ) ;
#53420=VERTEX_POINT ( 'NONE', #129304 ) ;
#53421=ADVANCED_FACE ( 'NONE', ( #41589 ), #29995, .F. ) ;
#53422=EDGE_LOOP ( 'NONE', ( #35821, #26605, #69273, #143306 ) ) ;
#53425=AXIS2_PLACEMENT_3D ( 'NONE', #109669, #95219, #30711 ) ;
#53426=EDGE_LOOP ( 'NONE', ( #60534, #50947, #77247, #82423 ) ) ;
#53427=ORIENTED_EDGE ( 'NONE', *, *, #79843, .T. ) ;
#53429=DIRECTION ( 'NONE',  ( 0.7071067811865486830, -0.7071067811865464625, -0.000000000000000000 ) ) ;
#53431=CARTESIAN_POINT ( 'NONE',  ( -20.70025512860841133, -27.71228299555191654, 4.000000000000000000 ) ) ;
#53432=CARTESIAN_POINT ( 'NONE',  ( -48.18398860626899705, 28.73617430169820608, 5.000000000000000000 ) ) ;
#53433=ORIENTED_EDGE ( 'NONE', *, *, #52063, .F. ) ;
#53434=DIRECTION ( 'NONE',  ( -0.000000000000000000, -0.3543493200069152693, 0.9351131265310292928 ) ) ;
#53435=VECTOR ( 'NONE', #34417, 1000.000000000000227 ) ;
#53436=PLANE ( 'NONE',  #86398 ) ;
#53439=PLANE ( 'NONE',  #8128 ) ;
#53440=AXIS2_PLACEMENT_3D ( 'NONE', #115385, #94383, #28441 ) ;
#53441=ORIENTED_EDGE ( 'NONE', *, *, #82804, .T. ) ;
#53442=CARTESIAN_POINT ( 'NONE',  ( 41.99451991528749062, 28.92564299267967343, 4.000000000000000000 ) ) ;
#53443=ORIENTED_EDGE ( 'NONE', *, *, #8506, .T. ) ;
#53444=ORIENTED_EDGE ( 'NONE', *, *, #76936, .T. ) ;
#53445=EDGE_LOOP ( 'NONE', ( #43294, #15096, #8904, #129294 ) ) ;
#53447=ADVANCED_FACE ( 'NONE', ( #119146 ), #64071, .F. ) ;
#53449=AXIS2_PLACEMENT_3D ( 'NONE', #112169, #114288, #25124 ) ;
#53450=ORIENTED_EDGE ( 'NONE', *, *, #90615, .T. ) ;
#53451=VECTOR ( 'NONE', #116777, 1000.000000000000000 ) ;
#53454=DIRECTION ( 'NONE',  ( -0.000000000000000000, 0.000000000000000000, 1.000000000000000000 ) ) ;
#53455=LINE ( 'NONE', #41145, #103365 ) ;
#53456=DIRECTION ( 'NONE',  ( -0.7071067811865487940, 0.7071067811865463515, -0.000000000000000000 ) ) ;
#53457=EDGE_CURVE ( 'NONE', #57200, #65937, #134334, .T. ) ;
#53458=ORIENTED_EDGE ( 'NONE', *, *, #30466, .F. ) ;
#53459=DIRECTION ( 'NONE',  ( -0.6830127018922181881, 0.6830127018922202975, -0.2588190451025214056 ) ) ;
#53460=VECTOR ( 'NONE', #31613, 999.9999999999998863 ) ;
#53462=EDGE_CURVE ( 'NONE', #39389, #14857, #5006, .T. ) ;
#53463=ADVANCED_FACE ( 'NONE', ( #38401 ), #55347, .T. ) ;
#53464=EDGE_CURVE ( 'NONE', #1086, #118931, #78519, .T. ) ;
#53466=DIRECTION ( 'NONE',  ( 0.7071067811865487940, 0.7071067811865463515, -0.000000000000000000 ) ) ;
#53467=EDGE_CURVE ( 'NONE', #65462, #92329, #2341, .T. ) ;
#53468=DIRECTION ( 'NONE',  ( -0.7071067811865486830, -0.7071067811865464625, 0.000000000000000000 ) ) ;
#53470=LINE ( 'NONE', #29554, #79140 ) ;
#53471=ORIENTED_EDGE ( 'NONE', *, *, #40849, .T. ) ;
#53472=ORIENTED_EDGE ( 'NONE', *, *, #74815, .T. ) ;
#53473=EDGE_CURVE ( 'NONE', #138697, #41182, #126812, .T. ) ;
#53474=VERTEX_POINT ( 'NONE', #27495 ) ;
#53475=DIRECTION ( 'NONE',  ( -0.6830127018922180770, -0.6830127018922204085, -0.2588190451025213501 ) ) ;
#53478=ADVANCED_FACE ( 'NONE', ( #56806 ), #45905, .F. ) ;
#53479=DIRECTION ( 'NONE',  ( 0.7071067811865487940, 0.7071067811865463515, 0.000000000000000000 ) ) ;
#53480=PLANE ( 'NONE',  #85318 ) ;
#53481=LINE ( 'NONE', #131042, #68859 ) ;
#53482=VECTOR ( 'NONE', #98848, 1000.000000000000227 ) ;
#53483=EDGE_CURVE ( 'NONE', #86990, #35713, #89386, .T. ) ;
#53484=AXIS2_PLACEMENT_3D ( 'NONE', #111865, #68387, #121991 ) ;
#53485=LINE ( 'NONE', #54230, #20571 ) ;
#53489=EDGE_LOOP ( 'NONE', ( #58774, #35975, #131126, #77004 ) ) ;
#53490=LINE ( 'NONE', #122281, #122918 ) ;
#53493=AXIS2_PLACEMENT_3D ( 'NONE', #79043, #34092, #131976 ) ;
#53494=ORIENTED_EDGE ( 'NONE', *, *, #21425, .F. ) ;
#53495=EDGE_CURVE ( 'NONE', #16426, #85226, #69086, .T. ) ;
#53496=DIRECTION ( 'NONE',  ( -0.7071067811865487940, 0.7071067811865463515, -0.000000000000000000 ) ) ;
#53497=DIRECTION ( 'NONE',  ( 0.7071067811865487940, -0.7071067811865463515, 0.000000000000000000 ) ) ;
#53498=ORIENTED_EDGE ( 'NONE', *, *, #36775, .T. ) ;
#53499=LINE ( 'NONE', #142646, #530 ) ;
#53501=LINE ( 'NONE', #9221, #13614 ) ;
#53502=ORIENTED_EDGE ( 'NONE', *, *, #61422, .F. ) ;
#53503=LINE ( 'NONE', #43342, #4973 ) ;
#53505=VERTEX_POINT ( 'NONE', #135074 ) ;
#53506=ADVANCED_FACE ( 'NONE', ( #49305 ), #24840, .T. ) ;
#53507=CARTESIAN_POINT ( 'NONE',  ( 20.99451991528748707, 28.92564299267952777, 4.000000000000000000 ) ) ;
#53509=CARTESIAN_POINT ( 'NONE',  ( -4.499999999999962697, -20.53675388469230967, 2.352720554255882224 ) ) ;
#53514=DIRECTION ( 'NONE',  ( 0.7071067811865486830, -0.7071067811865464625, -0.000000000000000000 ) ) ;
#53516=AXIS2_PLACEMENT_3D ( 'NONE', #29444, #73682, #140360 ) ;
#53520=CARTESIAN_POINT ( 'NONE',  ( 24.84463820744543838, 1.742823668393624903, 4.000000000000000000 ) ) ;
#53521=EDGE_LOOP ( 'NONE', ( #23742, #61328, #140865, #116073 ) ) ;
#53522=ORIENTED_EDGE ( 'NONE', *, *, #105533, .F. ) ;
#53523=LINE ( 'NONE', #142670, #16592 ) ;
#53524=ORIENTED_EDGE ( 'NONE', *, *, #131921, .T. ) ;
#53525=VECTOR ( 'NONE', #96897, 1000.000000000000000 ) ;
#53526=EDGE_CURVE ( 'NONE', #75102, #33478, #90088, .T. ) ;
#53527=DIRECTION ( 'NONE',  ( -0.7071067811865487940, 0.7071067811865463515, 0.000000000000000000 ) ) ;
#53529=VECTOR ( 'NONE', #47101, 1000.000000000000000 ) ;
#53530=ORIENTED_EDGE ( 'NONE', *, *, #58232, .F. ) ;
#53531=CARTESIAN_POINT ( 'NONE',  ( -30.75860074219774631, 21.72500000000000142, 5.000000000000000000 ) ) ;
#53532=DIRECTION ( 'NONE',  ( -0.7071067811865487940, -0.7071067811865463515, -0.000000000000000000 ) ) ;
#53533=EDGE_CURVE ( 'NONE', #32425, #79691, #111107, .T. ) ;
#53534=LINE ( 'NONE', #141989, #83602 ) ;
#53536=CARTESIAN_POINT ( 'NONE',  ( -6.005480084712508493, 28.92564299267933947, 4.000000000000000000 ) ) ;
#53538=CARTESIAN_POINT ( 'NONE',  ( 66.18398860626901126, 28.73617430169833753, 5.000000000000000000 ) ) ;
#53539=DIRECTION ( 'NONE',  ( -0.7071067811865486830, -0.7071067811865464625, -0.000000000000000000 ) ) ;
#53540=AXIS2_PLACEMENT_3D ( 'NONE', #88128, #116639, #6394 ) ;
#53541=CARTESIAN_POINT ( 'NONE',  ( -4.499999999999968914, -2.173586137069142499, -4.605770156576121543 ) ) ;
#53542=CARTESIAN_POINT ( 'NONE',  ( 7.499999999999947597, 14.14708470758592007, -0.5283514160166723483 ) ) ;
#53544=CARTESIAN_POINT ( 'NONE',  ( -13.62823445044376491, -8.240707523384200428, 11.38925528200755721 ) ) ;
#53545=VERTEX_POINT ( 'NONE', #123481 ) ;
#53549=( BOUNDED_CURVE ( )  B_SPLINE_CURVE ( 3, ( #11991, #34481, #122916, #112746 ),
 .UNSPECIFIED., .F., .T. ) 
 B_SPLINE_CURVE_WITH_KNOTS ( ( 4, 4 ),
 ( 1.864375635226932282, 1.933014472006540752 ),
 .UNSPECIFIED. ) 
 CURVE ( )  GEOMETRIC_REPRESENTATION_ITEM ( )  RATIONAL_B_SPLINE_CURVE ( ( 1.000000000000000000, 0.9996074310407765395, 0.9996074310407765395, 1.000000000000000000 ) ) 
 REPRESENTATION_ITEM ( '' )  );
#53550=VERTEX_POINT ( 'NONE', #112568 ) ;
#53551=EDGE_CURVE ( 'NONE', #141006, #17257, #23401, .T. ) ;
#53554=ORIENTED_EDGE ( 'NONE', *, *, #18063, .T. ) ;
#53555=AXIS2_PLACEMENT_3D ( 'NONE', #123915, #47108, #36185 ) ;
#53559=VECTOR ( 'NONE', #143086, 999.9999999999998863 ) ;
#53561=EDGE_LOOP ( 'NONE', ( #74697, #21930, #399, #89825 ) ) ;
#53564=VECTOR ( 'NONE', #103235, 1000.000000000000227 ) ;
#53565=CARTESIAN_POINT ( 'NONE',  ( -27.48921356237309155, -27.52281430457074762, 5.000000000000000000 ) ) ;
#53568=AXIS2_PLACEMENT_3D ( 'NONE', #112644, #135146, #35840 ) ;
#53569=EDGE_LOOP ( 'NONE', ( #58590, #91661, #76066, #1388 ) ) ;
#53570=ORIENTED_EDGE ( 'NONE', *, *, #137772, .F. ) ;
#53571=EDGE_CURVE ( 'NONE', #2765, #85157, #24137, .T. ) ;
#53572=EDGE_LOOP ( 'NONE', ( #89817, #124928, #70544, #100703 ) ) ;
#53573=FACE_OUTER_BOUND ( 'NONE', #73312, .T. ) ;
#53574=EDGE_CURVE ( 'NONE', #43296, #68456, #101684, .T. ) ;
#53577=FACE_OUTER_BOUND ( 'NONE', #54343, .T. ) ;
#53578=AXIS2_PLACEMENT_3D ( 'NONE', #82269, #126446, #5372 ) ;
#53580=PLANE ( 'NONE',  #23232 ) ;
#53582=VERTEX_POINT ( 'NONE', #77808 ) ;
#53583=ORIENTED_EDGE ( 'NONE', *, *, #67790, .T. ) ;
#53584=VECTOR ( 'NONE', #84463, 1000.000000000000000 ) ;
#53585=EDGE_CURVE ( 'NONE', #108392, #40720, #66930, .T. ) ;
#53586=CARTESIAN_POINT ( 'NONE',  ( -45.29974487139158867, -27.71228299555237840, 4.000000000000000000 ) ) ;
#53588=ORIENTED_EDGE ( 'NONE', *, *, #80356, .T. ) ;
#53590=EDGE_CURVE ( 'NONE', #114247, #68937, #52811, .T. ) ;
#53592=VECTOR ( 'NONE', #28951, 1000.000000000000227 ) ;
#53593=DIRECTION ( 'NONE',  ( 0.7071067811865487940, 0.7071067811865463515, 0.000000000000000000 ) ) ;
#53594=EDGE_CURVE ( 'NONE', #141614, #125764, #50004, .T. ) ;
#53595=ORIENTED_EDGE ( 'NONE', *, *, #96986, .F. ) ;
#53596=CARTESIAN_POINT ( 'NONE',  ( -34.92500000000001137, -22.22500000000000142, 4.000000000000000000 ) ) ;
#53598=AXIS2_PLACEMENT_3D ( 'NONE', #75900, #20790, #9916 ) ;
#53599=CARTESIAN_POINT ( 'NONE',  ( 8.187538124160473885, -22.22500000000000142, 4.000000000000000000 ) ) ;
#53600=CARTESIAN_POINT ( 'NONE',  ( -45.48921356237309510, -27.52281430457087197, 5.000000000000000000 ) ) ;
#53601=AXIS2_PLACEMENT_3D ( 'NONE', #91164, #37488, #26597 ) ;
#53602=CARTESIAN_POINT ( 'NONE',  ( 65.99451991528749772, 28.92564299267984396, 4.000000000000000000 ) ) ;
#53603=ORIENTED_EDGE ( 'NONE', *, *, #102486, .F. ) ;
#53606=CARTESIAN_POINT ( 'NONE',  ( -8.207106781186485733, 0.7592924766157138627, 5.000000000000000000 ) ) ;
#53607=ORIENTED_EDGE ( 'NONE', *, *, #142669, .F. ) ;
#53608=AXIS2_PLACEMENT_3D ( 'NONE', #124099, #11736, #133559 ) ;
#53609=CARTESIAN_POINT ( 'NONE',  ( -14.99451991528749595, 28.92564299267948513, 4.000000000000000000 ) ) ;
#53610=EDGE_CURVE ( 'NONE', #136709, #115243, #94891, .T. ) ;
#53612=DIRECTION ( 'NONE',  ( -0.000000000000000000, -0.3543493200069152693, 0.9351131265310292928 ) ) ;
#53613=ORIENTED_EDGE ( 'NONE', *, *, #142016, .T. ) ;
#53614=ORIENTED_EDGE ( 'NONE', *, *, #34279, .F. ) ;
#53615=ORIENTED_EDGE ( 'NONE', *, *, #85879, .F. ) ;
#53616=( BOUNDED_CURVE ( )  B_SPLINE_CURVE ( 3, ( #23504, #25643, #70631, #68478 ),
 .UNSPECIFIED., .F., .T. ) 
 B_SPLINE_CURVE_WITH_KNOTS ( ( 4, 4 ),
 ( 4.350170835173026163, 4.500739107949217832 ),
 .UNSPECIFIED. ) 
 CURVE ( )  GEOMETRIC_REPRESENTATION_ITEM ( )  RATIONAL_B_SPLINE_CURVE ( ( 1.000000000000000000, 0.9981116584018955296, 0.9981116584018955296, 1.000000000000000000 ) ) 
 REPRESENTATION_ITEM ( '' )  );
#53617=DIRECTION ( 'NONE',  ( -0.000000000000000000, 0.000000000000000000, 1.000000000000000000 ) ) ;
#53618=LINE ( 'NONE', #118853, #62323 ) ;
#53619=CARTESIAN_POINT ( 'NONE',  ( 0.000000000000000000, 0.000000000000000000, 5.000000000000000000 ) ) ;
#53620=CARTESIAN_POINT ( 'NONE',  ( -34.49999999999975131, -4.535744391599457082, 4.994342998332168548 ) ) ;
#53621=DIRECTION ( 'NONE',  ( 0.6830127018922181881, 0.6830127018922202975, -0.2588190451025214056 ) ) ;
#53622=DIRECTION ( 'NONE',  ( 0.3543493200069163240, 0.000000000000000000, 0.9351131265310288487 ) ) ;
#53624=LINE ( 'NONE', #7209, #66660 ) ;
#53626=DIRECTION ( 'NONE',  ( -0.7071067811865486830, -0.7071067811865464625, -0.000000000000000000 ) ) ;
#53627=DIRECTION ( 'NONE',  ( -0.000000000000000000, -0.3543493200069152693, 0.9351131265310292928 ) ) ;
#53628=LINE ( 'NONE', #131897, #38983 ) ;
#53629=LINE ( 'NONE', #43455, #130441 ) ;
#53630=ORIENTED_EDGE ( 'NONE', *, *, #57757, .F. ) ;
#53631=VERTEX_POINT ( 'NONE', #106464 ) ;
#53632=ORIENTED_EDGE ( 'NONE', *, *, #66655, .T. ) ;
#53633=VECTOR ( 'NONE', #137104, 1000.000000000000000 ) ;
#53634=ORIENTED_EDGE ( 'NONE', *, *, #47782, .T. ) ;
#53636=ORIENTED_EDGE ( 'NONE', *, *, #105398, .F. ) ;
#53637=ORIENTED_EDGE ( 'NONE', *, *, #101009, .F. ) ;
#53638=CARTESIAN_POINT ( 'NONE',  ( -12.29974487139158512, -27.71228299555214747, 4.000000000000000000 ) ) ;
#53639=DIRECTION ( 'NONE',  ( 1.000000000000000000, 0.000000000000000000, 0.000000000000000000 ) ) ;
#53640=VERTEX_POINT ( 'NONE', #97009 ) ;
#53641=LINE ( 'NONE', #97852, #129783 ) ;
#53642=AXIS2_PLACEMENT_3D ( 'NONE', #50123, #94319, #107338 ) ;
#53644=PLANE ( 'NONE',  #86252 ) ;
#53645=FACE_OUTER_BOUND ( 'NONE', #47211, .T. ) ;
#53650=EDGE_CURVE ( 'NONE', #62423, #138332, #60911, .T. ) ;
#53652=EDGE_CURVE ( 'NONE', #117341, #3772, #84756, .T. ) ;
#53653=CARTESIAN_POINT ( 'NONE',  ( 36.48921356237310221, -27.52281430457080802, 5.000000000000000000 ) ) ;
#53654=CARTESIAN_POINT ( 'NONE',  ( -27.71757738642548574, -21.73023691814493574, 5.000000000000000888 ) ) ;
#53656=EDGE_LOOP ( 'NONE', ( #64472, #126685, #67031, #41532 ) ) ;
#53657=ADVANCED_FACE ( 'NONE', ( #17348 ), #130418, .F. ) ;
#53658=CARTESIAN_POINT ( 'NONE',  ( -7.499999999999942268, -1.533600742197722910, 5.000000000000000000 ) ) ;
#53659=ORIENTED_EDGE ( 'NONE', *, *, #105014, .T. ) ;
#53660=DIRECTION ( 'NONE',  ( -0.7071067811865486830, 0.7071067811865464625, 0.000000000000000000 ) ) ;
#53661=CARTESIAN_POINT ( 'NONE',  ( 28.82816939922333432, -17.24070752338409918, 4.000000000000000000 ) ) ;
#53663=VECTOR ( 'NONE', #94970, 1000.000000000000000 ) ;
#53664=DIRECTION ( 'NONE',  ( 0.000000000000000000, 0.000000000000000000, -1.000000000000000000 ) ) ;
#53665=EDGE_CURVE ( 'NONE', #1213, #42638, #108583, .T. ) ;
#53666=PLANE ( 'NONE',  #42634 ) ;
#53667=VERTEX_POINT ( 'NONE', #39856 ) ;
#53669=DIRECTION ( 'NONE',  ( 0.3543493200069162685, -0.000000000000000000, -0.9351131265310288487 ) ) ;
#53671=EDGE_CURVE ( 'NONE', #58614, #99505, #7148, .T. ) ;
#53672=CARTESIAN_POINT ( 'NONE',  ( -10.49999999999993250, 3.653845994658382779, -4.504631822206345504 ) ) ;
#53673=CARTESIAN_POINT ( 'NONE',  ( -34.49999999999975842, -7.535744391599424219, 4.994342998332167660 ) ) ;
#53674=EDGE_LOOP ( 'NONE', ( #32195, #94305, #87038, #20451 ) ) ;
#53675=CARTESIAN_POINT ( 'NONE',  ( -48.18398860626899705, 28.73617430169820608, 5.000000000000000000 ) ) ;
#53677=VECTOR ( 'NONE', #98446, 1000.000000000000227 ) ;
#53678=VECTOR ( 'NONE', #14970, 1000.000000000000000 ) ;
#53679=VECTOR ( 'NONE', #117874, 1000.000000000000000 ) ;
#53680=CARTESIAN_POINT ( 'NONE',  ( -13.29703526515639567, -22.22500000000000142, 13.19564433381002466 ) ) ;
#53681=VECTOR ( 'NONE', #83373, 999.9999999999998863 ) ;
#53683=EDGE_CURVE ( 'NONE', #63651, #64860, #84076, .T. ) ;
#53684=FACE_OUTER_BOUND ( 'NONE', #71153, .T. ) ;
#53685=ORIENTED_EDGE ( 'NONE', *, *, #29664, .T. ) ;
#53686=ORIENTED_EDGE ( 'NONE', *, *, #100375, .T. ) ;
#53687=ADVANCED_FACE ( 'NONE', ( #138428 ), #62305, .F. ) ;
#53688=CARTESIAN_POINT ( 'NONE',  ( -4.828169399223495084, -8.240707523384198652, 4.000000000000000000 ) ) ;
#53689=LINE ( 'NONE', #117465, #129425 ) ;
#53691=DIRECTION ( 'NONE',  ( 0.6830127018922180770, 0.6830127018922202975, -0.2588190451025213501 ) ) ;
#53693=DIRECTION ( 'NONE',  ( -0.000000000000000000, -0.3543493200069152693, 0.9351131265310292928 ) ) ;
#53694=CARTESIAN_POINT ( 'NONE',  ( 57.18398860626899705, 28.73617430169827358, 5.000000000000000000 ) ) ;
#53697=LINE ( 'NONE', #131969, #14751 ) ;
#53698=CARTESIAN_POINT ( 'NONE',  ( 5.816011393731002066, 28.73617430169783304, 5.000000000000000000 ) ) ;
#53699=EDGE_CURVE ( 'NONE', #90846, #17453, #29637, .T. ) ;
#53700=DIRECTION ( 'NONE',  ( 0.7071067811865486830, -0.7071067811865464625, -0.000000000000000000 ) ) ;
#53701=CARTESIAN_POINT ( 'NONE',  ( -21.29974487139158512, -27.71228299555221142, 4.000000000000000000 ) ) ;
#53702=CARTESIAN_POINT ( 'NONE',  ( -15.18398860626900237, 28.73617430169797871, 5.000000000000000000 ) ) ;
#53703=FACE_OUTER_BOUND ( 'NONE', #50714, .T. ) ;
#53704=DIRECTION ( 'NONE',  ( -0.000000000000000000, 0.000000000000000000, 1.000000000000000000 ) ) ;
#53705=ORIENTED_EDGE ( 'NONE', *, *, #69563, .T. ) ;
#53706=VECTOR ( 'NONE', #24520, 1000.000000000000000 ) ;
#53707=ORIENTED_EDGE ( 'NONE', *, *, #27435, .T. ) ;
#53708=ORIENTED_EDGE ( 'NONE', *, *, #82333, .F. ) ;
#53710=ORIENTED_EDGE ( 'NONE', *, *, #112206, .T. ) ;
#53711=ORIENTED_EDGE ( 'NONE', *, *, #22225, .T. ) ;
#53712=VECTOR ( 'NONE', #39751, 1000.000000000000000 ) ;
#53713=ORIENTED_EDGE ( 'NONE', *, *, #91441, .F. ) ;
#53714=ADVANCED_FACE ( 'NONE', ( #73882 ), #18760, .T. ) ;
#53715=PLANE ( 'NONE',  #92019 ) ;
#53716=FACE_OUTER_BOUND ( 'NONE', #137962, .T. ) ;
#53720=CARTESIAN_POINT ( 'NONE',  ( 32.99999999999977263, 19.55218569542897100, 5.000000000000000000 ) ) ;
#53721=FACE_OUTER_BOUND ( 'NONE', #108666, .T. ) ;
#53722=DIRECTION ( 'NONE',  ( -0.7071067811865486830, -0.7071067811865464625, -0.000000000000000000 ) ) ;
#53723=EDGE_LOOP ( 'NONE', ( #101941, #123544, #123939, #38160 ) ) ;
#53725=DIRECTION ( 'NONE',  ( -0.7071067811865486830, 0.7071067811865464625, 0.000000000000000000 ) ) ;
#53726=CARTESIAN_POINT ( 'NONE',  ( 39.29974487139159578, -27.71228299555233576, 4.000000000000000000 ) ) ;
#53728=AXIS2_PLACEMENT_3D ( 'NONE', #125650, #137233, #26328 ) ;
#53730=CARTESIAN_POINT ( 'NONE',  ( 71.99451991528749772, 28.92564299267988304, 4.000000000000000000 ) ) ;
#53732=EDGE_CURVE ( 'NONE', #15939, #9981, #139155, .T. ) ;
#53733=FACE_OUTER_BOUND ( 'NONE', #108904, .T. ) ;
#53734=ORIENTED_EDGE ( 'NONE', *, *, #56518, .T. ) ;
#53735=ORIENTED_EDGE ( 'NONE', *, *, #79193, .T. ) ;
#53737=ORIENTED_EDGE ( 'NONE', *, *, #35829, .F. ) ;
#53738=PLANE ( 'NONE',  #71841 ) ;
#53739=EDGE_CURVE ( 'NONE', #48205, #332, #51429, .T. ) ;
#53740=VECTOR ( 'NONE', #76015, 1000.000000000000000 ) ;
#53744=DIRECTION ( 'NONE',  ( -0.7071067811865487940, 0.7071067811865463515, 0.000000000000000000 ) ) ;
#53746=CARTESIAN_POINT ( 'NONE',  ( -26.38161509397988169, -2.240707523384264377, 13.37739548510245235 ) ) ;
#53748=ORIENTED_EDGE ( 'NONE', *, *, #53590, .T. ) ;
#53749=ADVANCED_FACE ( 'NONE', ( #73189 ), #117352, .F. ) ;
#53750=ORIENTED_EDGE ( 'NONE', *, *, #75621, .F. ) ;
#53751=VECTOR ( 'NONE', #20458, 1000.000000000000227 ) ;
#53752=LINE ( 'NONE', #43564, #78656 ) ;
#53753=FACE_OUTER_BOUND ( 'NONE', #4893, .T. ) ;
#53755=PLANE ( 'NONE',  #92787 ) ;
#53756=ORIENTED_EDGE ( 'NONE', *, *, #109268, .T. ) ;
#53758=EDGE_CURVE ( 'NONE', #38491, #19628, #581, .T. ) ;
#53759=VERTEX_POINT ( 'NONE', #133282 ) ;
#53760=DIRECTION ( 'NONE',  ( 1.000000000000000000, 0.000000000000000000, 0.000000000000000000 ) ) ;
#53762=CARTESIAN_POINT ( 'NONE',  ( -34.49999999999976552, -8.945670655168967755, 4.994342998332164996 ) ) ;
#53763=FACE_OUTER_BOUND ( 'NONE', #35173, .T. ) ;
#53766=EDGE_LOOP ( 'NONE', ( #29627, #18421, #72324, #140589, #29025 ) ) ;
#53767=CARTESIAN_POINT ( 'NONE',  ( -33.70710678118631165, -9.740707523384180888, 5.000000000000000000 ) ) ;
#53769=ORIENTED_EDGE ( 'NONE', *, *, #142550, .F. ) ;
#53770=VECTOR ( 'NONE', #137300, 1000.000000000000000 ) ;
#53771=ORIENTED_EDGE ( 'NONE', *, *, #110966, .F. ) ;
#53772=AXIS2_PLACEMENT_3D ( 'NONE', #143420, #23796, #88352 ) ;
#53774=VECTOR ( 'NONE', #75525, 999.9999999999998863 ) ;
#53776=EDGE_CURVE ( 'NONE', #114717, #11535, #65171, .T. ) ;
#53777=EDGE_LOOP ( 'NONE', ( #28010, #20485, #112257, #16756 ) ) ;
#53778=CARTESIAN_POINT ( 'NONE',  ( 24.18398860626899705, 28.73617430169804265, 5.000000000000000000 ) ) ;
#53779=AXIS2_PLACEMENT_3D ( 'NONE', #61937, #5361, #7507 ) ;
#53780=CARTESIAN_POINT ( 'NONE',  ( 6.299744871391586898, -27.71228299555210484, 4.000000000000000000 ) ) ;
#53783=FACE_OUTER_BOUND ( 'NONE', #41743, .T. ) ;
#53784=LINE ( 'NONE', #56665, #5001 ) ;
#53785=EDGE_CURVE ( 'NONE', #21943, #12779, #75325, .T. ) ;
#53786=FACE_BOUND ( 'NONE', #55206, .T. ) ;
#53788=DIRECTION ( 'NONE',  ( 1.000000000000000000, -0.000000000000000000, -0.000000000000000000 ) ) ;
#53789=CARTESIAN_POINT ( 'NONE',  ( 9.489213562373095101, -27.52281430457062328, 5.000000000000000000 ) ) ;
#53790=EDGE_CURVE ( 'NONE', #7267, #60163, #20906, .T. ) ;
#53791=ORIENTED_EDGE ( 'NONE', *, *, #109907, .T. ) ;
#53792=FACE_OUTER_BOUND ( 'NONE', #21991, .T. ) ;
#53793=EDGE_LOOP ( 'NONE', ( #76245, #120339, #111435, #71526 ) ) ;
#53794=ORIENTED_EDGE ( 'NONE', *, *, #12810, .F. ) ;
#53796=VERTEX_POINT ( 'NONE', #33964 ) ;
#53798=ORIENTED_EDGE ( 'NONE', *, *, #32765, .T. ) ;
#53799=CARTESIAN_POINT ( 'NONE',  ( 21.48921356237309155, -27.52281430457070499, 5.000000000000000000 ) ) ;
#53800=VERTEX_POINT ( 'NONE', #119491 ) ;
#53801=DIRECTION ( 'NONE',  ( 1.000000000000000000, 0.000000000000000000, 0.000000000000000000 ) ) ;
#53803=LINE ( 'NONE', #85676, #58417 ) ;
#53804=DIRECTION ( 'NONE',  ( -0.7071067811865486830, -0.7071067811865464625, 0.000000000000000000 ) ) ;
#53805=EDGE_CURVE ( 'NONE', #68252, #51146, #67303, .T. ) ;
#53806=VECTOR ( 'NONE', #59518, 1000.000000000000227 ) ;
#53807=LINE ( 'NONE', #117575, #117255 ) ;
#53808=DIRECTION ( 'NONE',  ( 0.7071067811865487940, -0.7071067811865463515, 0.000000000000000000 ) ) ;
#53809=DIRECTION ( 'NONE',  ( -0.7071067811865487940, 0.7071067811865463515, 0.000000000000000000 ) ) ;
#53810=VECTOR ( 'NONE', #95354, 1000.000000000000227 ) ;
#53811=DIRECTION ( 'NONE',  ( -0.6830127018922181881, 0.6830127018922202975, -0.2588190451025214056 ) ) ;
#53812=CARTESIAN_POINT ( 'NONE',  ( 24.48921356237309510, -27.52281430457072631, 5.000000000000000000 ) ) ;
#53813=ORIENTED_EDGE ( 'NONE', *, *, #11518, .F. ) ;
#53814=ORIENTED_EDGE ( 'NONE', *, *, #27130, .F. ) ;
#53815=ORIENTED_EDGE ( 'NONE', *, *, #42029, .F. ) ;
#53818=DIRECTION ( 'NONE',  ( -0.7071067811865486830, -0.7071067811865464625, 0.000000000000000000 ) ) ;
#53820=ORIENTED_EDGE ( 'NONE', *, *, #3721, .T. ) ;
#53821=DIRECTION ( 'NONE',  ( 0.7071067811865486830, -0.7071067811865464625, -0.000000000000000000 ) ) ;
#53822=FACE_OUTER_BOUND ( 'NONE', #106688, .T. ) ;
#53823=CARTESIAN_POINT ( 'NONE',  ( 33.18398860626899705, 28.73617430169810305, 5.000000000000000000 ) ) ;
#53824=VERTEX_POINT ( 'NONE', #142708 ) ;
#53825=DIRECTION ( 'NONE',  ( 0.7071067811865487940, 0.7071067811865463515, -0.000000000000000000 ) ) ;
#53827=DIRECTION ( 'NONE',  ( -0.7071067811865486830, -0.7071067811865464625, 0.000000000000000000 ) ) ;
#53829=EDGE_CURVE ( 'NONE', #115943, #51894, #78178, .T. ) ;
#53830=CARTESIAN_POINT ( 'NONE',  ( -11.99999999999992006, -10.77435723561696435, -9.972017380717201007 ) ) ;
#53831=VERTEX_POINT ( 'NONE', #100643 ) ;
#53833=EDGE_CURVE ( 'NONE', #73333, #128893, #89061, .T. ) ;
#53834=CARTESIAN_POINT ( 'NONE',  ( -21.48921356237309155, -27.52281430457070499, 5.000000000000000000 ) ) ;
#53835=VECTOR ( 'NONE', #31466, 999.9999999999998863 ) ;
#53836=FACE_OUTER_BOUND ( 'NONE', #21774, .T. ) ;
#53837=DIRECTION ( 'NONE',  ( -0.6830127018922180770, -0.6830127018922204085, -0.2588190451025213501 ) ) ;
#53838=VERTEX_POINT ( 'NONE', #98484 ) ;
#53839=LINE ( 'NONE', #98042, #120259 ) ;
#53841=ORIENTED_EDGE ( 'NONE', *, *, #740, .F. ) ;
#53842=CARTESIAN_POINT ( 'NONE',  ( -17.81601139373099940, 28.73617430169775133, 5.000000000000000000 ) ) ;
#53843=DIRECTION ( 'NONE',  ( -0.6830127018922181881, 0.6830127018922202975, -0.2588190451025214056 ) ) ;
#53844=ADVANCED_FACE ( 'NONE', ( #88342 ), #99914, .F. ) ;
#53845=EDGE_CURVE ( 'NONE', #28815, #122724, #122355, .T. ) ;
#53846=CARTESIAN_POINT ( 'NONE',  ( -31.06996025486389712, -0.7407075233842735917, 13.87443053587618458 ) ) ;
#53847=( BOUNDED_CURVE ( )  B_SPLINE_CURVE ( 3, ( #124384, #36649, #137412, #2578 ),
 .UNSPECIFIED., .F., .F. ) 
 B_SPLINE_CURVE_WITH_KNOTS ( ( 4, 4 ),
 ( 1.975938068165228767, 2.025325302527091420 ),
 .UNSPECIFIED. ) 
 CURVE ( )  GEOMETRIC_REPRESENTATION_ITEM ( )  RATIONAL_B_SPLINE_CURVE ( ( 1.000000000000000000, 0.9997967520851089862, 0.9997967520851089862, 1.000000000000000000 ) ) 
 REPRESENTATION_ITEM ( '' )  );
#53848=EDGE_LOOP ( 'NONE', ( #22871, #141548, #88049, #49243 ) ) ;
#53850=LINE ( 'NONE', #42972, #53751 ) ;
#53851=ORIENTED_EDGE ( 'NONE', *, *, #71808, .T. ) ;
#53852=VECTOR ( 'NONE', #76390, 1000.000000000000000 ) ;
#53853=PLANE ( 'NONE',  #99496 ) ;
#53854=( BOUNDED_CURVE ( )  B_SPLINE_CURVE ( 3, ( #103770, #60326, #48717, #71923 ),
 .UNSPECIFIED., .F., .T. ) 
 B_SPLINE_CURVE_WITH_KNOTS ( ( 4, 4 ),
 ( 5.043186909253412509, 5.074607125596364732 ),
 .UNSPECIFIED. ) 
 CURVE ( )  GEOMETRIC_REPRESENTATION_ITEM ( )  RATIONAL_B_SPLINE_CURVE ( ( 1.000000000000000000, 0.9999177325257868620, 0.9999177325257868620, 1.000000000000000000 ) ) 
 REPRESENTATION_ITEM ( '' )  );
#53855=CARTESIAN_POINT ( 'NONE',  ( -29.67183060077625711, 2.259292476615694323, 4.000000000000000000 ) ) ;
#53856=ORIENTED_EDGE ( 'NONE', *, *, #15251, .F. ) ;
#53857=CARTESIAN_POINT ( 'NONE',  ( -9.489213562373095101, -27.52281430457062328, 5.000000000000000000 ) ) ;
#53858=EDGE_CURVE ( 'NONE', #37853, #27739, #120942, .T. ) ;
#53859=CARTESIAN_POINT ( 'NONE',  ( -13.43359823057990354, 1.153863645259229909, 4.000000000000000000 ) ) ;
#53860=VERTEX_POINT ( 'NONE', #21646 ) ;
#53861=EDGE_CURVE ( 'NONE', #13100, #67034, #89748, .T. ) ;
#53863=AXIS2_PLACEMENT_3D ( 'NONE', #107367, #17498, #6581 ) ;
#53864=LINE ( 'NONE', #7450, #72786 ) ;
#53865=CARTESIAN_POINT ( 'NONE',  ( 34.92499999999998295, 18.66246187583882588, 4.000000000000000000 ) ) ;
#53866=EDGE_CURVE ( 'NONE', #13798, #127597, #20181, .T. ) ;
#53867=CARTESIAN_POINT ( 'NONE',  ( -23.20710678118638626, -11.24070752338416312, 5.000000000000000000 ) ) ;
#53868=LINE ( 'NONE', #119089, #32264 ) ;
#53869=DIRECTION ( 'NONE',  ( -0.7071067811865486830, -0.7071067811865464625, 0.000000000000000000 ) ) ;
#53871=CARTESIAN_POINT ( 'NONE',  ( -12.45006917115538947, -22.22500000000000142, 13.51659144808220425 ) ) ;
#53872=CARTESIAN_POINT ( 'NONE',  ( -37.25154412867552622, -11.24070752338416490, 10.39518518046017981 ) ) ;
#53873=CARTESIAN_POINT ( 'NONE',  ( -2.700255128608413990, -27.71228299555204089, 4.000000000000000000 ) ) ;
#53875=EDGE_CURVE ( 'NONE', #25399, #96412, #110055, .T. ) ;
#53876=VECTOR ( 'NONE', #20462, 1000.000000000000000 ) ;
#53877=VECTOR ( 'NONE', #16446, 1000.000000000000000 ) ;
#53878=CARTESIAN_POINT ( 'NONE',  ( 33.18398860626899705, 28.73617430169810305, 5.000000000000000000 ) ) ;
#53880=CARTESIAN_POINT ( 'NONE',  ( 31.88982677111766506, -22.22500000000000142, 4.785647885939354751 ) ) ;
#53881=VECTOR ( 'NONE', #43831, 1000.000000000000000 ) ;
#53882=VECTOR ( 'NONE', #15221, 1000.000000000000000 ) ;
#53884=ORIENTED_EDGE ( 'NONE', *, *, #42105, .T. ) ;
#53885=CARTESIAN_POINT ( 'NONE',  ( 3.792893218813436551, -8.240707523384196875, 5.000000000000000000 ) ) ;
#53886=VERTEX_POINT ( 'NONE', #77479 ) ;
#53887=ORIENTED_EDGE ( 'NONE', *, *, #110063, .F. ) ;
#53890=VECTOR ( 'NONE', #116091, 1000.000000000000000 ) ;
#53891=DIRECTION ( 'NONE',  ( 1.000000000000000000, 0.000000000000000000, 0.000000000000000000 ) ) ;
#53892=CARTESIAN_POINT ( 'NONE',  ( 32.28242261357411280, -21.73023691814492508, 5.000000000000000888 ) ) ;
#53893=ORIENTED_EDGE ( 'NONE', *, *, #13336, .T. ) ;
#53894=CARTESIAN_POINT ( 'NONE',  ( -25.49999999999982236, -16.91253812416058366, 4.000000000000000000 ) ) ;
#53895=DIRECTION ( 'NONE',  ( 0.7071067811865487940, 0.7071067811865463515, -0.000000000000000000 ) ) ;
#53896=DIRECTION ( 'NONE',  ( 0.000000000000000000, -1.000000000000000000, 0.000000000000000000 ) ) ;
#53897=LINE ( 'NONE', #74198, #34923 ) ;
#53899=ORIENTED_EDGE ( 'NONE', *, *, #62336, .T. ) ;
#53902=CARTESIAN_POINT ( 'NONE',  ( -6.989119713460464567, -22.02621442084248216, 4.990779571109223767 ) ) ;
#53903=ADVANCED_FACE ( 'NONE', ( #25193 ), #115033, .F. ) ;
#53904=DIRECTION ( 'NONE',  ( -0.000000000000000000, 0.3543493200069153248, 0.9351131265310292928 ) ) ;
#53905=DIRECTION ( 'NONE',  ( 0.7071067811865487940, 0.7071067811865463515, 0.000000000000000000 ) ) ;
#53906=CARTESIAN_POINT ( 'NONE',  ( 29.99999999999980105, -16.44781430457066662, 5.000000000000000000 ) ) ;
#53907=FACE_OUTER_BOUND ( 'NONE', #85596, .T. ) ;
#53908=DIRECTION ( 'NONE',  ( -0.7071067811865486830, -0.7071067811865464625, 0.000000000000000000 ) ) ;
#53910=EDGE_CURVE ( 'NONE', #88704, #116329, #3430, .T. ) ;
#53911=VECTOR ( 'NONE', #51174, 1000.000000000000000 ) ;
#53912=FACE_OUTER_BOUND ( 'NONE', #143018, .T. ) ;
#53913=VERTEX_POINT ( 'NONE', #102058 ) ;
#53914=ORIENTED_EDGE ( 'NONE', *, *, #127986, .F. ) ;
#53916=CARTESIAN_POINT ( 'NONE',  ( 21.71238017851529989, 8.518175273744143183, 4.330735335516821216 ) ) ;
#53917=CARTESIAN_POINT ( 'NONE',  ( 14.20710678118645376, -2.240707523384257716, 5.000000000000000000 ) ) ;
#53918=DIRECTION ( 'NONE',  ( -0.6830127018922180770, -0.6830127018922204085, -0.2588190451025213501 ) ) ;
#53919=VERTEX_POINT ( 'NONE', #46288 ) ;
#53920=CARTESIAN_POINT ( 'NONE',  ( -75.48921356237309510, -27.52281430457107803, 5.000000000000000000 ) ) ;
#53921=AXIS2_PLACEMENT_3D ( 'NONE', #50057, #94249, #138489 ) ;
#53922=CARTESIAN_POINT ( 'NONE',  ( 72.18398860626899705, 28.73617430169837661, 5.000000000000000000 ) ) ;
#53924=VECTOR ( 'NONE', #69920, 1000.000000000000000 ) ;
#53925=ORIENTED_EDGE ( 'NONE', *, *, #10418, .F. ) ;
#53927=ORIENTED_EDGE ( 'NONE', *, *, #40918, .F. ) ;
#53928=AXIS2_PLACEMENT_3D ( 'NONE', #8213, #6769, #95251 ) ;
#53930=DIRECTION ( 'NONE',  ( -0.7071067811865486830, 0.7071067811865464625, 0.000000000000000000 ) ) ;
#53931=CARTESIAN_POINT ( 'NONE',  ( 4.499999999999979572, 6.052185695429108669, 5.000000000000000000 ) ) ;
#53932=CARTESIAN_POINT ( 'NONE',  ( 78.29974487139158157, -27.71228299555260577, 4.000000000000000000 ) ) ;
#53933=LINE ( 'NONE', #98126, #76480 ) ;
#53934=ORIENTED_EDGE ( 'NONE', *, *, #50225, .F. ) ;
#53935=DIRECTION ( 'NONE',  ( 0.6830127018922181881, 0.6830127018922202975, -0.2588190451025214056 ) ) ;
#53936=FACE_OUTER_BOUND ( 'NONE', #24365, .T. ) ;
#53937=ORIENTED_EDGE ( 'NONE', *, *, #142724, .T. ) ;
#53939=LINE ( 'NONE', #76388, #67061 ) ;
#53940=DIRECTION ( 'NONE',  ( -0.000000000000000000, -0.3543493200069152693, 0.9351131265310292928 ) ) ;
#53941=CARTESIAN_POINT ( 'NONE',  ( 19.21071296386495675, 9.141836041257182188, 4.000000000000000000 ) ) ;
#53942=DIRECTION ( 'NONE',  ( -0.7071067811865487940, 0.7071067811865463515, -0.000000000000000000 ) ) ;
#53943=CARTESIAN_POINT ( 'NONE',  ( 0.000000000000000000, 0.000000000000000000, 5.000000000000000000 ) ) ;
#53944=VECTOR ( 'NONE', #121051, 1000.000000000000000 ) ;
#53945=ORIENTED_EDGE ( 'NONE', *, *, #75869, .T. ) ;
#53948=CARTESIAN_POINT ( 'NONE',  ( 36.18398860626899705, 28.73617430169812437, 5.000000000000000000 ) ) ;
#53949=EDGE_CURVE ( 'NONE', #100985, #46950, #35414, .T. ) ;
#53950=PLANE ( 'NONE',  #12996 ) ;
#53951=ORIENTED_EDGE ( 'NONE', *, *, #30948, .T. ) ;
#53952=ORIENTED_EDGE ( 'NONE', *, *, #53998, .F. ) ;
#53955=DIRECTION ( 'NONE',  ( -0.7071067811865486830, -0.7071067811865464625, -0.000000000000000000 ) ) ;
#53956=ORIENTED_EDGE ( 'NONE', *, *, #87489, .F. ) ;
#53958=LINE ( 'NONE', #120575, #76903 ) ;
#53959=ORIENTED_EDGE ( 'NONE', *, *, #103380, .T. ) ;
#53960=FACE_OUTER_BOUND ( 'NONE', #111330, .T. ) ;
#53961=DIRECTION ( 'NONE',  ( 0.7071067811865487940, -0.7071067811865463515, 0.000000000000000000 ) ) ;
#53962=VECTOR ( 'NONE', #136108, 1000.000000000000000 ) ;
#53964=EDGE_CURVE ( 'NONE', #19920, #45152, #59305, .T. ) ;
#53965=FACE_BOUND ( 'NONE', #40978, .T. ) ;
#53966=PLANE ( 'NONE',  #34009 ) ;
#53967=FACE_OUTER_BOUND ( 'NONE', #68921, .T. ) ;
#53968=ADVANCED_FACE ( 'NONE', ( #124526 ), #26636, .F. ) ;
#53971=PLANE ( 'NONE',  #136140 ) ;
#53974=ORIENTED_EDGE ( 'NONE', *, *, #125199, .F. ) ;
#53977=ORIENTED_EDGE ( 'NONE', *, *, #67997, .T. ) ;
#53978=EDGE_CURVE ( 'NONE', #130020, #55512, #123487, .T. ) ;
#53979=DIRECTION ( 'NONE',  ( 0.6830127018922180770, -0.6830127018922204085, -0.2588190451025213501 ) ) ;
#53980=ORIENTED_EDGE ( 'NONE', *, *, #14020, .F. ) ;
#53981=CARTESIAN_POINT ( 'NONE',  ( 28.63753812416078048, 22.22499999999999432, 4.000000000000000000 ) ) ;
#53982=VECTOR ( 'NONE', #68157, 1000.000000000000000 ) ;
#53983=AXIS2_PLACEMENT_3D ( 'NONE', #72602, #116756, #39952 ) ;
#53984=EDGE_CURVE ( 'NONE', #48060, #95984, #125962, .T. ) ;
#53986=CARTESIAN_POINT ( 'NONE',  ( 30.08314806772912320, 21.75929247661549581, 7.311836541448121451 ) ) ;
#53987=CARTESIAN_POINT ( 'NONE',  ( 20.66989781452722141, 17.25929247661553845, 19.83885114516066750 ) ) ;
#53988=DIRECTION ( 'NONE',  ( -0.7071067811865487940, 0.7071067811865463515, -0.000000000000000000 ) ) ;
#53990=LINE ( 'NONE', #141694, #112089 ) ;
#53991=LINE ( 'NONE', #54690, #95544 ) ;
#53992=FACE_OUTER_BOUND ( 'NONE', #76653, .T. ) ;
#53994=AXIS2_PLACEMENT_3D ( 'NONE', #80053, #103871, #125670 ) ;
#53996=EDGE_CURVE ( 'NONE', #46307, #120604, #78906, .T. ) ;
#53998=EDGE_CURVE ( 'NONE', #59677, #27437, #136820, .T. ) ;
#53999=ORIENTED_EDGE ( 'NONE', *, *, #82807, .T. ) ;
#54001=DIRECTION ( 'NONE',  ( 0.000000000000000000, -0.3543493200069153248, 0.9351131265310292928 ) ) ;
#54003=ORIENTED_EDGE ( 'NONE', *, *, #138817, .T. ) ;
#54005=VERTEX_POINT ( 'NONE', #47028 ) ;
#54006=CARTESIAN_POINT ( 'NONE',  ( 32.50183651486023706, -17.24070752338409918, 8.407044977365149663 ) ) ;
#54007=LINE ( 'NONE', #111186, #107138 ) ;
#54011=ORIENTED_EDGE ( 'NONE', *, *, #54253, .T. ) ;
#54012=EDGE_CURVE ( 'NONE', #72227, #11858, #9517, .T. ) ;
#54015=CARTESIAN_POINT ( 'NONE',  ( -39.48921356237310221, -27.52281430457082934, 5.000000000000000000 ) ) ;
#54016=LINE ( 'NONE', #10458, #51728 ) ;
#54017=EDGE_LOOP ( 'NONE', ( #69020, #64772, #126262, #133854 ) ) ;
#54018=VERTEX_POINT ( 'NONE', #15028 ) ;
#54019=LINE ( 'NONE', #130862, #12504 ) ;
#54022=EDGE_CURVE ( 'NONE', #42968, #93122, #69451, .T. ) ;
#54023=EDGE_CURVE ( 'NONE', #57857, #124559, #92584, .T. ) ;
#54024=DIRECTION ( 'NONE',  ( -0.6830127018922180770, -0.6830127018922204085, -0.2588190451025213501 ) ) ;
#54025=EDGE_LOOP ( 'NONE', ( #36240, #45863, #29602 ) ) ;
#54027=VERTEX_POINT ( 'NONE', #14328 ) ;
#54028=PRODUCT ( '1.3 Jaw Plate', '1.3 Jaw Plate', '', ( #15554 ) ) ;
#54030=AXIS2_PLACEMENT_3D ( 'NONE', #40126, #84341, #94455 ) ;
#54031=VERTEX_POINT ( 'NONE', #103461 ) ;
#54033=LINE ( 'NONE', #32249, #32456 ) ;
#54034=DIRECTION ( 'NONE',  ( -0.7071067811865486830, -0.7071067811865464625, -0.000000000000000000 ) ) ;
#54035=EDGE_CURVE ( 'NONE', #29880, #71067, #123834, .T. ) ;
#54038=VECTOR ( 'NONE', #37250, 1000.000000000000000 ) ;
#54039=CARTESIAN_POINT ( 'NONE',  ( 8.700255128608413102, -27.71228299555199825, 4.000000000000000000 ) ) ;
#54040=ADVANCED_FACE ( 'NONE', ( #57165 ), #135428, .F. ) ;
#54041=DIRECTION ( 'NONE',  ( -0.7071067811865486830, 0.7071067811865464625, 0.000000000000000000 ) ) ;
#54042=ORIENTED_EDGE ( 'NONE', *, *, #18884, .F. ) ;
#54043=EDGE_CURVE ( 'NONE', #31547, #92519, #25928, .T. ) ;
#54045=ORIENTED_EDGE ( 'NONE', *, *, #95666, .F. ) ;
#54046=DIRECTION ( 'NONE',  ( -0.3543493200069162685, -0.000000000000000000, -0.9351131265310288487 ) ) ;
#54047=( BOUNDED_CURVE ( )  B_SPLINE_CURVE ( 3, ( #121417, #122125, #67808, #101813 ),
 .UNSPECIFIED., .F., .T. ) 
 B_SPLINE_CURVE_WITH_KNOTS ( ( 4, 4 ),
 ( 1.864375635226937389, 1.933014472006547635 ),
 .UNSPECIFIED. ) 
 CURVE ( )  GEOMETRIC_REPRESENTATION_ITEM ( )  RATIONAL_B_SPLINE_CURVE ( ( 1.000000000000000000, 0.9996074310407765395, 0.9996074310407765395, 1.000000000000000000 ) ) 
 REPRESENTATION_ITEM ( '' )  );
#54048=AXIS2_PLACEMENT_3D ( 'NONE', #122213, #113480, #67150 ) ;
#54049=DIRECTION ( 'NONE',  ( -0.7071067811865486830, 0.7071067811865464625, 0.000000000000000000 ) ) ;
#54050=VECTOR ( 'NONE', #107661, 1000.000000000000227 ) ;
#54051=ORIENTED_EDGE ( 'NONE', *, *, #16288, .T. ) ;
#54052=FACE_OUTER_BOUND ( 'NONE', #30006, .T. ) ;
#54053=DIRECTION ( 'NONE',  ( -0.000000000000000000, 0.000000000000000000, 1.000000000000000000 ) ) ;
#54054=ADVANCED_FACE ( 'NONE', ( #80336 ), #138257, .F. ) ;
#54056=EDGE_LOOP ( 'NONE', ( #119334, #142786, #109330, #14121 ) ) ;
#54057=EDGE_LOOP ( 'NONE', ( #6625, #81416, #35237, #10949 ) ) ;
#54058=CARTESIAN_POINT ( 'NONE',  ( -8.994519915287490619, 28.92564299267944250, 4.000000000000000000 ) ) ;
#54059=LINE ( 'NONE', #121403, #141417 ) ;
#54060=LINE ( 'NONE', #128723, #102537 ) ;
#54062=EDGE_CURVE ( 'NONE', #114666, #105677, #105594, .T. ) ;
#54063=LINE ( 'NONE', #11924, #138490 ) ;
#54065=DIRECTION ( 'NONE',  ( 0.000000000000000000, 1.000000000000000000, -0.000000000000000000 ) ) ;
#54066=CARTESIAN_POINT ( 'NONE',  ( 26.99999999999981526, -0.2811185226894025169, -5.995736974527575924 ) ) ;
#54069=EDGE_LOOP ( 'NONE', ( #78544, #90509, #105367, #89212 ) ) ;
#54070=DIRECTION ( 'NONE',  ( 0.7071067811865487940, 0.7071067811865463515, 0.000000000000000000 ) ) ;
#54071=VERTEX_POINT ( 'NONE', #51258 ) ;
#54073=FACE_OUTER_BOUND ( 'NONE', #20558, .T. ) ;
#54074=DIRECTION ( 'NONE',  ( -0.000000000000000000, -0.3543493200069152693, 0.9351131265310292928 ) ) ;
#54077=CARTESIAN_POINT ( 'NONE',  ( 8.999999999999944933, -4.447814304570779420, 5.000000000000000000 ) ) ;
#54078=ORIENTED_EDGE ( 'NONE', *, *, #102272, .F. ) ;
#54080=CARTESIAN_POINT ( 'NONE',  ( -34.92500000000001137, 22.22500000000000142, 4.000000000000000000 ) ) ;
#54081=DIRECTION ( 'NONE',  ( -0.7071067811865486830, -0.7071067811865464625, -0.000000000000000000 ) ) ;
#54082=ORIENTED_EDGE ( 'NONE', *, *, #28185, .F. ) ;
#54084=VERTEX_POINT ( 'NONE', #38942 ) ;
#54085=DIRECTION ( 'NONE',  ( 0.3543493200069162685, -0.000000000000000000, -0.9351131265310288487 ) ) ;
#54087=EDGE_CURVE ( 'NONE', #95860, #12218, #72332, .T. ) ;
#54088=DIRECTION ( 'NONE',  ( -0.000000000000000000, 0.3543493200069153248, 0.9351131265310292928 ) ) ;
#54089=CARTESIAN_POINT ( 'NONE',  ( -0.7228143045705931469, -21.72500000000000142, 5.000000000000000000 ) ) ;
#54090=ADVANCED_FACE ( 'NONE', ( #29473 ), #7717, .F. ) ;
#54092=PLANE ( 'NONE',  #125069 ) ;
#54093=EDGE_CURVE ( 'NONE', #75982, #9218, #39195, .T. ) ;
#54094=VECTOR ( 'NONE', #11314, 1000.000000000000227 ) ;
#54095=LINE ( 'NONE', #43193, #113181 ) ;
#54096=ORIENTED_EDGE ( 'NONE', *, *, #35124, .T. ) ;
#54098=DIRECTION ( 'NONE',  ( 0.7071067811865487940, 0.7071067811865463515, 0.000000000000000000 ) ) ;
#54099=DIRECTION ( 'NONE',  ( -0.7071067811865486830, 0.7071067811865464625, 0.000000000000000000 ) ) ;
#54101=ORIENTED_EDGE ( 'NONE', *, *, #70704, .F. ) ;
#54102=EDGE_CURVE ( 'NONE', #19820, #42524, #18578, .T. ) ;
#54103=VECTOR ( 'NONE', #120250, 1000.000000000000227 ) ;
#54104=FACE_OUTER_BOUND ( 'NONE', #71088, .T. ) ;
#54105=ORIENTED_EDGE ( 'NONE', *, *, #29621, .T. ) ;
#54107=VECTOR ( 'NONE', #89752, 999.9999999999998863 ) ;
#54108=CARTESIAN_POINT ( 'NONE',  ( -29.95341186370437825, 14.25929247661557042, 18.84478104361334871 ) ) ;
#54111=CARTESIAN_POINT ( 'NONE',  ( 15.75860074219783513, 21.72499999999999432, 5.000000000000000000 ) ) ;
#54112=CARTESIAN_POINT ( 'NONE',  ( 8.510786437626906675, -27.52281430457049183, 5.000000000000000000 ) ) ;
#54113=CARTESIAN_POINT ( 'NONE',  ( 9.046588136295392601, 14.25929247661557042, 18.84478104361325634 ) ) ;
#54114=CARTESIAN_POINT ( 'NONE',  ( 11.29289321881338104, -9.740707523384184441, 5.000000000000000000 ) ) ;
#54115=LINE ( 'NONE', #33082, #8193 ) ;
#54118=LINE ( 'NONE', #107018, #33749 ) ;
#54119=FACE_OUTER_BOUND ( 'NONE', #72053, .T. ) ;
#54120=CIRCLE ( 'NONE', #135139, 3.378199999999994319 ) ;
#54121=CARTESIAN_POINT ( 'NONE',  ( -12.70710678118645909, 11.25929247661560773, 5.000000000000000000 ) ) ;
#54122=ORIENTED_EDGE ( 'NONE', *, *, #61176, .T. ) ;
#54125=VECTOR ( 'NONE', #99291, 1000.000000000000227 ) ;
#54126=ORIENTED_EDGE ( 'NONE', *, *, #36818, .T. ) ;
#54127=CARTESIAN_POINT ( 'NONE',  ( 15.18398860626900237, 28.73617430169797871, 5.000000000000000000 ) ) ;
#54128=CARTESIAN_POINT ( 'NONE',  ( 2.816011393730999401, 28.73617430169785436, 5.000000000000000000 ) ) ;
#54130=EDGE_CURVE ( 'NONE', #62418, #59656, #17864, .T. ) ;
#54131=CARTESIAN_POINT ( 'NONE',  ( -69.18398860626899705, 28.73617430169835529, 5.000000000000000000 ) ) ;
#54132=LINE ( 'NONE', #97581, #20024 ) ;
#54133=EDGE_LOOP ( 'NONE', ( #121548, #104422, #121667, #73401 ) ) ;
#54134=VERTEX_POINT ( 'NONE', #118632 ) ;
#54135=DIRECTION ( 'NONE',  ( -0.7071067811865486830, -0.7071067811865464625, -0.000000000000000000 ) ) ;
#54137=ORIENTED_EDGE ( 'NONE', *, *, #34327, .T. ) ;
#54139=DIRECTION ( 'NONE',  ( 0.7071067811865487940, 0.7071067811865463515, 0.000000000000000000 ) ) ;
#54140=CARTESIAN_POINT ( 'NONE',  ( -7.889826771117836479, -22.22499999999999787, 4.785647885939353863 ) ) ;
#54141=ORIENTED_EDGE ( 'NONE', *, *, #23950, .F. ) ;
#54142=VECTOR ( 'NONE', #50994, 1000.000000000000000 ) ;
#54143=EDGE_CURVE ( 'NONE', #107847, #73688, #94716, .T. ) ;
#54144=EDGE_CURVE ( 'NONE', #70620, #60930, #6971, .T. ) ;
#54145=ADVANCED_FACE ( 'NONE', ( #28793 ), #62857, .T. ) ;
#54146=FACE_BOUND ( 'NONE', #102817, .T. ) ;
#54148=FACE_OUTER_BOUND ( 'NONE', #65209, .T. ) ;
#54150=CARTESIAN_POINT ( 'NONE',  ( -21.29974487139158512, -27.71228299555221142, 4.000000000000000000 ) ) ;
#54151=VECTOR ( 'NONE', #20045, 1000.000000000000000 ) ;
#54152=EDGE_CURVE ( 'NONE', #15997, #133006, #82456, .T. ) ;
#54154=DIRECTION ( 'NONE',  ( -0.000000000000000000, -0.3543493200069152693, 0.9351131265310292928 ) ) ;
#54157=VECTOR ( 'NONE', #59528, 1000.000000000000000 ) ;
#54158=VERTEX_POINT ( 'NONE', #17189 ) ;
#54160=EDGE_LOOP ( 'NONE', ( #135936, #121030, #13963, #139206 ) ) ;
#54161=EDGE_CURVE ( 'NONE', #72846, #123539, #115739, .T. ) ;
#54162=ORIENTED_EDGE ( 'NONE', *, *, #45574, .T. ) ;
#54163=AXIS2_PLACEMENT_3D ( 'NONE', #67988, #112857, #133912 ) ;
#54165=CARTESIAN_POINT ( 'NONE',  ( 19.17183060077634238, -14.24070752338414003, 4.000000000000000000 ) ) ;
#54167=DIRECTION ( 'NONE',  ( 0.7071067811865486830, 0.7071067811865463515, 0.000000000000000000 ) ) ;
#54170=DIRECTION ( 'NONE',  ( -0.7071067811865487940, 0.7071067811865463515, -0.000000000000000000 ) ) ;
#54171=FACE_OUTER_BOUND ( 'NONE', #107085, .T. ) ;
#54172=LINE ( 'NONE', #22190, #96548 ) ;
#54173=LINE ( 'NONE', #44737, #32258 ) ;
#54174=AXIS2_PLACEMENT_3D ( 'NONE', #48846, #93763, #38671 ) ;
#54175=EDGE_CURVE ( 'NONE', #103024, #79108, #43240, .T. ) ;
#54176=DIRECTION ( 'NONE',  ( 1.000000000000000000, 0.000000000000000000, 0.000000000000000000 ) ) ;
#54178=CARTESIAN_POINT ( 'NONE',  ( 60.18398860626900415, 28.73617430169829490, 5.000000000000000000 ) ) ;
#54179=LINE ( 'NONE', #98366, #115915 ) ;
#54180=ORIENTED_EDGE ( 'NONE', *, *, #41560, .F. ) ;
#54182=EDGE_LOOP ( 'NONE', ( #142535, #34199, #111271, #73068 ) ) ;
#54184=EDGE_CURVE ( 'NONE', #98472, #43787, #131671, .T. ) ;
#54185=EDGE_LOOP ( 'NONE', ( #61077, #84217, #81256, #35093 ) ) ;
#54186=CARTESIAN_POINT ( 'NONE',  ( 69.29974487139159578, -27.71228299555254537, 4.000000000000000000 ) ) ;
#54187=VECTOR ( 'NONE', #91282, 1000.000000000000227 ) ;
#54190=CARTESIAN_POINT ( 'NONE',  ( 34.92499999999998295, 6.759292476615656575, 4.255531930566160526 ) ) ;
#54191=CARTESIAN_POINT ( 'NONE',  ( -26.99999999999981526, -19.22509904557638549, 1.855685503482115584 ) ) ;
#54192=CARTESIAN_POINT ( 'NONE',  ( -22.49999999999984013, -14.56887692260766087, 4.000000000000000000 ) ) ;
#54193=EDGE_CURVE ( 'NONE', #79114, #106843, #67123, .T. ) ;
#54194=EDGE_LOOP ( 'NONE', ( #52028, #115560, #140251 ) ) ;
#54195=DIRECTION ( 'NONE',  ( -0.6830127018922181881, 0.6830127018922202975, -0.2588190451025214056 ) ) ;
#54196=CARTESIAN_POINT ( 'NONE',  ( 30.79289321881324781, -17.24070752338410628, 5.000000000000000000 ) ) ;
#54197=VECTOR ( 'NONE', #19357, 1000.000000000000000 ) ;
#54198=DIRECTION ( 'NONE',  ( 0.7071067811865487940, 0.7071067811865463515, -0.000000000000000000 ) ) ;
#54199=PLANE ( 'NONE',  #15074 ) ;
#54200=EDGE_CURVE ( 'NONE', #47328, #118264, #65739, .T. ) ;
#54201=EDGE_LOOP ( 'NONE', ( #95166, #135508, #7117 ) ) ;
#54202=LINE ( 'NONE', #52026, #92050 ) ;
#54203=ORIENTED_EDGE ( 'NONE', *, *, #138746, .T. ) ;
#54204=ADVANCED_FACE ( 'NONE', ( #55539 ), #10566, .F. ) ;
#54208=VERTEX_POINT ( 'NONE', #43943 ) ;
#54209=EDGE_CURVE ( 'NONE', #37150, #22300, #64997, .T. ) ;
#54210=CARTESIAN_POINT ( 'NONE',  ( -11.99451991528749417, 28.92564299267946382, 4.000000000000000000 ) ) ;
#54211=CARTESIAN_POINT ( 'NONE',  ( 34.49999999999975131, 13.46425560840035196, 4.994342998332160555 ) ) ;
#54213=DIRECTION ( 'NONE',  ( 0.7071067811865486830, -0.7071067811865464625, -0.000000000000000000 ) ) ;
#54215=VECTOR ( 'NONE', #41112, 1000.000000000000000 ) ;
#54218=DIRECTION ( 'NONE',  ( -0.7071067811865486830, -0.7071067811865464625, 0.000000000000000000 ) ) ;
#54220=EDGE_CURVE ( 'NONE', #88566, #69745, #404, .T. ) ;
#54222=ORIENTED_EDGE ( 'NONE', *, *, #141115, .T. ) ;
#54223=ORIENTED_EDGE ( 'NONE', *, *, #129485, .T. ) ;
#54224=ORIENTED_EDGE ( 'NONE', *, *, #119597, .F. ) ;
#54226=DIRECTION ( 'NONE',  ( -0.000000000000000000, 0.000000000000000000, 1.000000000000000000 ) ) ;
#54227=LINE ( 'NONE', #44035, #24191 ) ;
#54228=EDGE_CURVE ( 'NONE', #1839, #140728, #41799, .T. ) ;
#54229=CARTESIAN_POINT ( 'NONE',  ( 31.49999999999979039, 6.052185695429111334, 5.000000000000000000 ) ) ;
#54230=CARTESIAN_POINT ( 'NONE',  ( 34.92499999999998295, 22.22500000000000142, 4.500000000000000888 ) ) ;
#54231=AXIS2_PLACEMENT_3D ( 'NONE', #12274, #76863, #1375 ) ;
#54234=LINE ( 'NONE', #133900, #39674 ) ;
#54235=ORIENTED_EDGE ( 'NONE', *, *, #105688, .F. ) ;
#54237=EDGE_LOOP ( 'NONE', ( #101968, #41793, #128995, #115744, #57521 ) ) ;
#54238=CARTESIAN_POINT ( 'NONE',  ( 22.42819999999999681, 3.174999999999997158, 0.000000000000000000 ) ) ;
#54239=ORIENTED_EDGE ( 'NONE', *, *, #46964, .F. ) ;
#54243=ORIENTED_EDGE ( 'NONE', *, *, #34279, .T. ) ;
#54244=VECTOR ( 'NONE', #108153, 1000.000000000000000 ) ;
#54245=CARTESIAN_POINT ( 'NONE',  ( -19.41009064519819916, 9.759292476615618384, 11.28811694763774298 ) ) ;
#54246=EDGE_CURVE ( 'NONE', #117563, #5082, #42540, .T. ) ;
#54247=ORIENTED_EDGE ( 'NONE', *, *, #97396, .F. ) ;
#54248=CARTESIAN_POINT ( 'NONE',  ( 22.49999999999984013, -4.216083040037233332, -7.486842126848710421 ) ) ;
#54249=ORIENTED_EDGE ( 'NONE', *, *, #131278, .F. ) ;
#54250=PLANE ( 'NONE',  #39710 ) ;
#54251=VERTEX_POINT ( 'NONE', #32352 ) ;
#54252=VECTOR ( 'NONE', #140255, 1000.000000000000000 ) ;
#54253=EDGE_CURVE ( 'NONE', #110463, #98003, #33796, .T. ) ;
#54256=VECTOR ( 'NONE', #136526, 1000.000000000000000 ) ;
#54257=CARTESIAN_POINT ( 'NONE',  ( 14.70025512860841133, -27.71228299555195917, 4.000000000000000000 ) ) ;
#54258=CARTESIAN_POINT ( 'NONE',  ( 0.000000000000000000, 0.000000000000000000, 5.000000000000000000 ) ) ;
#54259=CARTESIAN_POINT ( 'NONE',  ( -8.999999999999932498, 14.96639925780211478, 5.000000000000000000 ) ) ;
#54262=LINE ( 'NONE', #11386, #141562 ) ;
#54263=DIRECTION ( 'NONE',  ( -0.6830127018922181881, 0.6830127018922202975, -0.2588190451025214056 ) ) ;
#54264=EDGE_LOOP ( 'NONE', ( #12124, #117482, #55300, #54224 ) ) ;
#54266=ADVANCED_FACE ( 'NONE', ( #54830 ), #99735, .F. ) ;
#54267=ORIENTED_EDGE ( 'NONE', *, *, #75838, .F. ) ;
#54268=EDGE_CURVE ( 'NONE', #72412, #79859, #75861, .T. ) ;
#54269=LINE ( 'NONE', #54963, #23540 ) ;
#54270=VERTEX_POINT ( 'NONE', #9107 ) ;
#54271=CARTESIAN_POINT ( 'NONE',  ( 54.18398860626899705, 28.73617430169825226, 5.000000000000000000 ) ) ;
#54272=DIRECTION ( 'NONE',  ( -0.3543493200069162685, -0.000000000000000000, -0.9351131265310288487 ) ) ;
#54273=VECTOR ( 'NONE', #34053, 1000.000000000000000 ) ;
#54274=LINE ( 'NONE', #110026, #8515 ) ;
#54275=VERTEX_POINT ( 'NONE', #88167 ) ;
#54276=CARTESIAN_POINT ( 'NONE',  ( -15.00548008471250228, 28.92564299267927552, 4.000000000000000000 ) ) ;
#54277=LINE ( 'NONE', #143383, #44217 ) ;
#54278=DIRECTION ( 'NONE',  ( 0.7071067811865487940, 0.7071067811865463515, -0.000000000000000000 ) ) ;
#54280=DIRECTION ( 'NONE',  ( -0.7071067811865486830, -0.7071067811865464625, 0.000000000000000000 ) ) ;
#54283=ORIENTED_EDGE ( 'NONE', *, *, #46495, .T. ) ;
#54284=LINE ( 'NONE', #97749, #90580 ) ;
#54285=LINE ( 'NONE', #140526, #133186 ) ;
#54287=DIRECTION ( 'NONE',  ( -0.6830127018922180770, -0.6830127018922204085, -0.2588190451025213501 ) ) ;
#54288=DIRECTION ( 'NONE',  ( -0.7071067811865486830, -0.7071067811865464625, 0.000000000000000000 ) ) ;
#54291=VERTEX_POINT ( 'NONE', #120025 ) ;
#54294=CARTESIAN_POINT ( 'NONE',  ( -19.05000000000000071, 3.174999999999997158, 1.444000000000000394 ) ) ;
#54297=CARTESIAN_POINT ( 'NONE',  ( 34.92499999999998295, -14.99387692260787652, 4.000000000000000000 ) ) ;
#54301=VERTEX_POINT ( 'NONE', #86011 ) ;
#54302=CARTESIAN_POINT ( 'NONE',  ( -29.99999999999979039, 18.08204922493370503, 0.9627537363045557406 ) ) ;
#54303=EDGE_CURVE ( 'NONE', #127190, #121732, #68856, .T. ) ;
#54304=DIRECTION ( 'NONE',  ( -0.3543493200069162685, -0.000000000000000000, -0.9351131265310288487 ) ) ;
#54305=ORIENTED_EDGE ( 'NONE', *, *, #112450, .F. ) ;
#54306=EDGE_LOOP ( 'NONE', ( #65215, #57029, #70334, #140365 ) ) ;
#54307=ORIENTED_EDGE ( 'NONE', *, *, #133980, .F. ) ;
#54308=CARTESIAN_POINT ( 'NONE',  ( 23.99999999999982947, 2.342191155542475034, -5.001666872980140788 ) ) ;
#54309=ADVANCED_FACE ( 'NONE', ( #30939 ), #75171, .F. ) ;
#54310=EDGE_CURVE ( 'NONE', #112531, #64780, #119330, .T. ) ;
#54311=DIRECTION ( 'NONE',  ( -0.7071067811865487940, 0.7071067811865463515, 0.000000000000000000 ) ) ;
#54313=CARTESIAN_POINT ( 'NONE',  ( -17.99451991528748351, 28.92564299267950645, 4.000000000000000000 ) ) ;
#54315=LINE ( 'NONE', #10742, #133580 ) ;
#54316=CARTESIAN_POINT ( 'NONE',  ( 34.47516574401890921, 12.02806734111568687, 4.998110765256834398 ) ) ;
#54317=EDGE_CURVE ( 'NONE', #102292, #47660, #24324, .T. ) ;
#54319=VECTOR ( 'NONE', #58760, 1000.000000000000114 ) ;
#54320=EDGE_CURVE ( 'NONE', #42461, #119756, #101409, .T. ) ;
#54321=ORIENTED_EDGE ( 'NONE', *, *, #96129, .F. ) ;
#54323=VECTOR ( 'NONE', #48170, 1000.000000000000000 ) ;
#54324=DIRECTION ( 'NONE',  ( 1.000000000000000000, 0.000000000000000000, 0.000000000000000000 ) ) ;
#54325=EDGE_CURVE ( 'NONE', #38343, #135502, #45398, .T. ) ;
#54326=ORIENTED_EDGE ( 'NONE', *, *, #53866, .F. ) ;
#54327=EDGE_LOOP ( 'NONE', ( #73506, #126197, #10842, #83667 ) ) ;
#54328=EDGE_CURVE ( 'NONE', #33187, #133473, #2542, .T. ) ;
#54330=DIRECTION ( 'NONE',  ( 0.7071067811865487940, 0.7071067811865463515, -0.000000000000000000 ) ) ;
#54331=ORIENTED_EDGE ( 'NONE', *, *, #25118, .T. ) ;
#54332=AXIS2_PLACEMENT_3D ( 'NONE', #19411, #117273, #30290 ) ;
#54333=CARTESIAN_POINT ( 'NONE',  ( -41.99451991528749062, 28.92564299267967343, 4.000000000000000000 ) ) ;
#54335=LINE ( 'NONE', #86224, #57195 ) ;
#54336=CARTESIAN_POINT ( 'NONE',  ( -27.48921356237309155, -27.52281430457074762, 5.000000000000000000 ) ) ;
#54338=ORIENTED_EDGE ( 'NONE', *, *, #29534, .F. ) ;
#54339=EDGE_CURVE ( 'NONE', #119913, #14862, #122929, .T. ) ;
#54340=LINE ( 'NONE', #142741, #78928 ) ;
#54341=ORIENTED_EDGE ( 'NONE', *, *, #76951, .T. ) ;
#54342=DIRECTION ( 'NONE',  ( -0.000000000000000000, 0.3543493200069153248, 0.9351131265310292928 ) ) ;
#54343=EDGE_LOOP ( 'NONE', ( #133265, #48706, #77176, #140648 ) ) ;
#54346=FACE_OUTER_BOUND ( 'NONE', #36577, .T. ) ;
#54347=VERTEX_POINT ( 'NONE', #124351 ) ;
#54348=ORIENTED_EDGE ( 'NONE', *, *, #66163, .T. ) ;
#54349=ADVANCED_FACE ( 'NONE', ( #46850 ), #14144, .F. ) ;
#54350=VERTEX_POINT ( 'NONE', #70719 ) ;
#54351=AXIS2_PLACEMENT_3D ( 'NONE', #116549, #61495, #50580 ) ;
#54352=LINE ( 'NONE', #21690, #16406 ) ;
#54354=VECTOR ( 'NONE', #129055, 1000.000000000000000 ) ;
#54355=CARTESIAN_POINT ( 'NONE',  ( 75.18398860626899705, 28.73617430169839793, 5.000000000000000000 ) ) ;
#54356=CARTESIAN_POINT ( 'NONE',  ( 10.49999999999993605, -17.94781430457064531, 5.000000000000000000 ) ) ;
#54358=DIRECTION ( 'NONE',  ( -0.7071067811865486830, 0.7071067811865464625, 0.000000000000000000 ) ) ;
#54359=CARTESIAN_POINT ( 'NONE',  ( -12.32816939922344268, 8.259292476615630818, 4.000000000000000000 ) ) ;
#54360=LINE ( 'NONE', #120993, #80638 ) ;
#54361=CARTESIAN_POINT ( 'NONE',  ( 34.42499999999998295, 0.000000000000000000, 4.500000000000000888 ) ) ;
#54362=VECTOR ( 'NONE', #136674, 999.9999999999998863 ) ;
#54363=LINE ( 'NONE', #43453, #108403 ) ;
#54364=EDGE_CURVE ( 'NONE', #131796, #135826, #90281, .T. ) ;
#54365=LINE ( 'NONE', #107953, #82978 ) ;
#54367=EDGE_LOOP ( 'NONE', ( #50380, #20086, #89901 ) ) ;
#54369=VERTEX_POINT ( 'NONE', #133804 ) ;
#54370=VERTEX_POINT ( 'NONE', #34491 ) ;
#54371=DIRECTION ( 'NONE',  ( -0.7071067811865486830, -0.7071067811865464625, 0.000000000000000000 ) ) ;
#54372=ORIENTED_EDGE ( 'NONE', *, *, #105529, .T. ) ;
#54373=EDGE_CURVE ( 'NONE', #8795, #110134, #78710, .T. ) ;
#54374=ORIENTED_EDGE ( 'NONE', *, *, #89328, .T. ) ;
#54375=DIRECTION ( 'NONE',  ( -0.7071067811865487940, 0.7071067811865463515, 0.000000000000000000 ) ) ;
#54377=CARTESIAN_POINT ( 'NONE',  ( -30.18398860626900060, 28.73617430169808173, 5.000000000000000000 ) ) ;
#54378=VERTEX_POINT ( 'NONE', #58437 ) ;
#54379=CARTESIAN_POINT ( 'NONE',  ( 6.299744871391586898, -27.71228299555210484, 4.000000000000000000 ) ) ;
#54380=ORIENTED_EDGE ( 'NONE', *, *, #48628, .F. ) ;
#54382=DIRECTION ( 'NONE',  ( -0.7071067811865487940, 0.7071067811865463515, -0.000000000000000000 ) ) ;
#54384=ORIENTED_EDGE ( 'NONE', *, *, #16345, .T. ) ;
#54386=DIRECTION ( 'NONE',  ( -0.000000000000000000, -0.3543493200069152693, 0.9351131265310292928 ) ) ;
#54387=CARTESIAN_POINT ( 'NONE',  ( -24.29974487139158867, -27.71228299555223273, 4.000000000000000000 ) ) ;
#54388=ADVANCED_FACE ( 'NONE', ( #72156 ), #49678, .F. ) ;
#54392=VERTEX_POINT ( 'NONE', #27166 ) ;
#54394=LINE ( 'NONE', #141364, #99582 ) ;
#54396=CARTESIAN_POINT ( 'NONE',  ( -3.770042794577900924, 21.73644205237997085, 5.000000000000000888 ) ) ;
#54397=DIRECTION ( 'NONE',  ( -0.000000000000000000, 0.000000000000000000, 1.000000000000000000 ) ) ;
#54398=VECTOR ( 'NONE', #10781, 1000.000000000000000 ) ;
#54399=ORIENTED_EDGE ( 'NONE', *, *, #94602, .F. ) ;
#54400=FACE_OUTER_BOUND ( 'NONE', #114612, .T. ) ;
#54401=ADVANCED_FACE ( 'NONE', ( #128637 ), #62678, .T. ) ;
#54404=FACE_OUTER_BOUND ( 'NONE', #116325, .T. ) ;
#54405=FACE_OUTER_BOUND ( 'NONE', #51545, .T. ) ;
#54406=ORIENTED_EDGE ( 'NONE', *, *, #84533, .T. ) ;
#54407=LINE ( 'NONE', #44235, #60315 ) ;
#54408=ORIENTED_EDGE ( 'NONE', *, *, #64594, .F. ) ;
#54409=ADVANCED_FACE ( 'NONE', ( #27888 ), #93856, .F. ) ;
#54411=CARTESIAN_POINT ( 'NONE',  ( -5.510786437626906675, -27.52281430457051314, 5.000000000000000000 ) ) ;
#54412=FACE_OUTER_BOUND ( 'NONE', #82498, .T. ) ;
#54413=EDGE_LOOP ( 'NONE', ( #47853, #48927, #14496, #73902, #50181 ) ) ;
#54415=DIRECTION ( 'NONE',  ( 0.7071067811865486830, -0.7071067811865464625, -0.000000000000000000 ) ) ;
#54417=EDGE_CURVE ( 'NONE', #63482, #73550, #105435, .T. ) ;
#54418=( BOUNDED_CURVE ( )  B_SPLINE_CURVE ( 3, ( #16589, #60879, #39075, #83301 ),
 .UNSPECIFIED., .F., .T. ) 
 B_SPLINE_CURVE_WITH_KNOTS ( ( 4, 4 ),
 ( 5.043186909253417838, 5.074607125596330093 ),
 .UNSPECIFIED. ) 
 CURVE ( )  GEOMETRIC_REPRESENTATION_ITEM ( )  RATIONAL_B_SPLINE_CURVE ( ( 1.000000000000000000, 0.9999177325257870841, 0.9999177325257870841, 1.000000000000000000 ) ) 
 REPRESENTATION_ITEM ( '' )  );
#54419=DIRECTION ( 'NONE',  ( 0.7071067811865487940, 0.7071067811865463515, 0.000000000000000000 ) ) ;
#54420=VECTOR ( 'NONE', #26948, 1000.000000000000000 ) ;
#54421=CARTESIAN_POINT ( 'NONE',  ( 33.18398860626899705, 28.73617430169810305, 5.000000000000000000 ) ) ;
#54422=FACE_OUTER_BOUND ( 'NONE', #115582, .T. ) ;
#54423=CARTESIAN_POINT ( 'NONE',  ( -34.92500000000001137, -8.337538124160923658, 4.000000000000000000 ) ) ;
#54424=CARTESIAN_POINT ( 'NONE',  ( -3.156123077392388065, -22.22500000000000142, 4.000000000000000000 ) ) ;
#54425=FACE_OUTER_BOUND ( 'NONE', #75210, .T. ) ;
#54426=DIRECTION ( 'NONE',  ( -0.000000000000000000, 0.3543493200069153248, 0.9351131265310292928 ) ) ;
#54427=CARTESIAN_POINT ( 'NONE',  ( 11.51078643762690490, -27.52281430457047406, 5.000000000000000000 ) ) ;
#54429=CARTESIAN_POINT ( 'NONE',  ( 19.78501580275798588, -3.740707523384238176, 15.76143240460128503 ) ) ;
#54430=ORIENTED_EDGE ( 'NONE', *, *, #68754, .F. ) ;
#54431=ADVANCED_FACE ( 'NONE', ( #38072 ), #137382, .T. ) ;
#54432=ORIENTED_EDGE ( 'NONE', *, *, #114682, .T. ) ;
#54434=ADVANCED_FACE ( 'NONE', ( #126473 ), #6091, .F. ) ;
#54435=VERTEX_POINT ( 'NONE', #61972 ) ;
#54437=ORIENTED_EDGE ( 'NONE', *, *, #101720, .T. ) ;
#54438=ORIENTED_EDGE ( 'NONE', *, *, #127837, .F. ) ;
#54439=PLANE ( 'NONE',  #114957 ) ;
#54440=DIRECTION ( 'NONE',  ( -0.7071067811865487940, 0.7071067811865463515, 0.000000000000000000 ) ) ;
#54441=ORIENTED_EDGE ( 'NONE', *, *, #106437, .T. ) ;
#54442=DIRECTION ( 'NONE',  ( 0.7071067811865487940, -0.7071067811865463515, 0.000000000000000000 ) ) ;
#54444=DIRECTION ( 'NONE',  ( -0.6830127018922181881, 0.6830127018922202975, -0.2588190451025214056 ) ) ;
#54445=CARTESIAN_POINT ( 'NONE',  ( -34.92500000000001137, -7.487538124160419528, 4.000000000000000000 ) ) ;
#54446=ORIENTED_EDGE ( 'NONE', *, *, #20971, .F. ) ;
#54449=CARTESIAN_POINT ( 'NONE',  ( 0.000000000000000000, 0.000000000000000000, 5.000000000000000000 ) ) ;
#54450=DIRECTION ( 'NONE',  ( 0.7071067811865487940, 0.7071067811865463515, 0.000000000000000000 ) ) ;
#54454=VECTOR ( 'NONE', #49641, 1000.000000000000227 ) ;
#54455=LINE ( 'NONE', #32693, #100164 ) ;
#54457=EDGE_LOOP ( 'NONE', ( #72443, #71643, #36860, #68650 ) ) ;
#54458=EDGE_LOOP ( 'NONE', ( #25464, #8016, #95300, #614 ) ) ;
#54460=ORIENTED_EDGE ( 'NONE', *, *, #62500, .F. ) ;
#54461=VECTOR ( 'NONE', #134030, 1000.000000000000000 ) ;
#54462=CARTESIAN_POINT ( 'NONE',  ( -63.48921356237309510, -27.52281430457099631, 5.000000000000000000 ) ) ;
#54463=DIRECTION ( 'NONE',  ( -0.7071067811865486830, -0.7071067811865464625, -0.000000000000000000 ) ) ;
#54464=CARTESIAN_POINT ( 'NONE',  ( -3.489213562373097322, -27.52281430457057709, 5.000000000000000000 ) ) ;
#54465=FACE_OUTER_BOUND ( 'NONE', #105236, .T. ) ;
#54466=CARTESIAN_POINT ( 'NONE',  ( -5.207106781186508826, 6.759292476615651246, 5.000000000000000000 ) ) ;
#54467=DIRECTION ( 'NONE',  ( -0.7071067811865486830, -0.7071067811865464625, -0.000000000000000000 ) ) ;
#54470=EDGE_CURVE ( 'NONE', #138219, #75105, #6806, .T. ) ;
#54471=ORIENTED_EDGE ( 'NONE', *, *, #48932, .T. ) ;
#54472=LINE ( 'NONE', #30566, #26991 ) ;
#54475=ORIENTED_EDGE ( 'NONE', *, *, #39453, .T. ) ;
#54476=DIRECTION ( 'NONE',  ( -0.7071067811865486830, 0.7071067811865464625, 0.000000000000000000 ) ) ;
#54477=EDGE_CURVE ( 'NONE', #2768, #139894, #106863, .T. ) ;
#54478=DIRECTION ( 'NONE',  ( -0.7071067811865486830, 0.7071067811865464625, 0.000000000000000000 ) ) ;
#54480=EDGE_CURVE ( 'NONE', #83105, #46795, #60559, .T. ) ;
#54482=EDGE_CURVE ( 'NONE', #861, #43029, #104732, .T. ) ;
#54483=EDGE_LOOP ( 'NONE', ( #108260, #88620, #32507, #91843 ) ) ;
#54484=FACE_OUTER_BOUND ( 'NONE', #14959, .T. ) ;
#54485=EDGE_CURVE ( 'NONE', #9764, #113899, #95990, .T. ) ;
#54486=ORIENTED_EDGE ( 'NONE', *, *, #116851, .T. ) ;
#54488=ORIENTED_EDGE ( 'NONE', *, *, #13415, .F. ) ;
#54489=EDGE_CURVE ( 'NONE', #96477, #60654, #23514, .T. ) ;
#54490=FACE_OUTER_BOUND ( 'NONE', #34708, .T. ) ;
#54491=EDGE_LOOP ( 'NONE', ( #142098, #24696, #48580, #38010 ) ) ;
#54493=EDGE_CURVE ( 'NONE', #106679, #106612, #40916, .T. ) ;
#54494=DIRECTION ( 'NONE',  ( -0.3543493200069162685, -0.000000000000000000, -0.9351131265310288487 ) ) ;
#54496=PLANE ( 'NONE',  #111522 ) ;
#54497=EDGE_CURVE ( 'NONE', #32541, #23207, #15541, .T. ) ;
#54498=FACE_BOUND ( 'NONE', #98266, .T. ) ;
#54499=ORIENTED_EDGE ( 'NONE', *, *, #4962, .T. ) ;
#54500=EDGE_CURVE ( 'NONE', #129291, #12567, #126392, .T. ) ;
#54501=PLANE ( 'NONE',  #24970 ) ;
#54502=PLANE ( 'NONE',  #5069 ) ;
#54503=CARTESIAN_POINT ( 'NONE',  ( -34.92500000000001137, -22.22500000000000142, 4.500000000000000888 ) ) ;
#54504=ORIENTED_EDGE ( 'NONE', *, *, #143448, .F. ) ;
#54505=FACE_OUTER_BOUND ( 'NONE', #27098, .T. ) ;
#54506=ORIENTED_EDGE ( 'NONE', *, *, #87304, .T. ) ;
#54508=EDGE_CURVE ( 'NONE', #118046, #62746, #82295, .T. ) ;
#54513=DIRECTION ( 'NONE',  ( -0.000000000000000000, -0.3543493200069152693, 0.9351131265310292928 ) ) ;
#54514=VECTOR ( 'NONE', #108420, 1000.000000000000000 ) ;
#54516=LINE ( 'NONE', #98696, #106593 ) ;
#54517=VERTEX_POINT ( 'NONE', #87982 ) ;
#54519=LINE ( 'NONE', #72191, #27308 ) ;
#54520=LINE ( 'NONE', #63276, #43310 ) ;
#54521=VECTOR ( 'NONE', #26745, 1000.000000000000000 ) ;
#54522=LINE ( 'NONE', #52349, #140764 ) ;
#54524=CARTESIAN_POINT ( 'NONE',  ( -66.18398860626901126, 28.73617430169833753, 5.000000000000000000 ) ) ;
#54525=LINE ( 'NONE', #129922, #20843 ) ;
#54526=EDGE_LOOP ( 'NONE', ( #118448, #96179, #41637, #64716 ) ) ;
#54528=ORIENTED_EDGE ( 'NONE', *, *, #95744, .T. ) ;
#54529=ORIENTED_EDGE ( 'NONE', *, *, #96512, .F. ) ;
#54530=CARTESIAN_POINT ( 'NONE',  ( 0.7071067811865406894, -12.74070752338415780, 5.000000000000000000 ) ) ;
#54533=ORIENTED_EDGE ( 'NONE', *, *, #40467, .F. ) ;
#54534=DIRECTION ( 'NONE',  ( 0.3543493200069162685, -0.000000000000000000, -0.9351131265310288487 ) ) ;
#54535=DIRECTION ( 'NONE',  ( -0.3543493200069162685, -0.000000000000000000, -0.9351131265310288487 ) ) ;
#54536=CARTESIAN_POINT ( 'NONE',  ( 45.48921356237309510, -27.52281430457087197, 5.000000000000000000 ) ) ;
#54537=ORIENTED_EDGE ( 'NONE', *, *, #13794, .T. ) ;
#54538=DIRECTION ( 'NONE',  ( -0.000000000000000000, -0.3543493200069152693, 0.9351131265310292928 ) ) ;
#54540=VECTOR ( 'NONE', #79796, 1000.000000000000000 ) ;
#54543=VECTOR ( 'NONE', #28930, 1000.000000000000000 ) ;
#54544=DIRECTION ( 'NONE',  ( 1.000000000000000000, 0.000000000000000000, 0.000000000000000000 ) ) ;
#54545=EDGE_LOOP ( 'NONE', ( #125056, #74122, #65238, #67233 ) ) ;
#54547=AXIS2_PLACEMENT_3D ( 'NONE', #64115, #117738, #141682 ) ;
#54548=PLANE ( 'NONE',  #41985 ) ;
#54550=DIRECTION ( 'NONE',  ( 0.7071067811865487940, 0.7071067811865463515, 0.000000000000000000 ) ) ;
#54551=LINE ( 'NONE', #8137, #118967 ) ;
#54552=VERTEX_POINT ( 'NONE', #132229 ) ;
#54554=ORIENTED_EDGE ( 'NONE', *, *, #90285, .T. ) ;
#54557=CARTESIAN_POINT ( 'NONE',  ( -5.994519915287488843, 28.92564299267942118, 4.000000000000000000 ) ) ;
#54558=DIRECTION ( 'NONE',  ( -0.000000000000000000, 0.000000000000000000, 1.000000000000000000 ) ) ;
#54560=EDGE_CURVE ( 'NONE', #38115, #123554, #121316, .T. ) ;
#54561=LINE ( 'NONE', #98049, #141415 ) ;
#54563=VERTEX_POINT ( 'NONE', #66248 ) ;
#54564=DIRECTION ( 'NONE',  ( 0.7071067811865487940, 0.7071067811865463515, 0.000000000000000000 ) ) ;
#54565=CARTESIAN_POINT ( 'NONE',  ( -6.792893218813409462, 0.7592924766157086447, 5.000000000000000000 ) ) ;
#54566=ORIENTED_EDGE ( 'NONE', *, *, #53462, .T. ) ;
#54567=LINE ( 'NONE', #132128, #43795 ) ;
#54568=DIRECTION ( 'NONE',  ( 0.7071067811865487940, 0.7071067811865463515, 0.000000000000000000 ) ) ;
#54569=ORIENTED_EDGE ( 'NONE', *, *, #2512, .F. ) ;
#54570=EDGE_CURVE ( 'NONE', #9775, #10888, #140919, .T. ) ;
#54571=ORIENTED_EDGE ( 'NONE', *, *, #35830, .F. ) ;
#54572=CARTESIAN_POINT ( 'NONE',  ( 17.51078643762690845, -27.52281430457043143, 5.000000000000000000 ) ) ;
#54574=VERTEX_POINT ( 'NONE', #20562 ) ;
#54575=CARTESIAN_POINT ( 'NONE',  ( 15.18398860626900237, 28.73617430169797871, 5.000000000000000000 ) ) ;
#54576=DIRECTION ( 'NONE',  ( 0.000000000000000000, 0.000000000000000000, -1.000000000000000000 ) ) ;
#54577=PLANE ( 'NONE',  #70039 ) ;
#54578=ORIENTED_EDGE ( 'NONE', *, *, #138110, .F. ) ;
#54579=DIRECTION ( 'NONE',  ( -0.7071067811865486830, -0.7071067811865464625, 0.000000000000000000 ) ) ;
#54580=CARTESIAN_POINT ( 'NONE',  ( -21.18398860626899349, 28.73617430169802134, 5.000000000000000000 ) ) ;
#54583=LINE ( 'NONE', #43688, #23358 ) ;
#54584=EDGE_CURVE ( 'NONE', #13816, #52329, #98843, .T. ) ;
#54585=ORIENTED_EDGE ( 'NONE', *, *, #1747, .F. ) ;
#54586=ORIENTED_EDGE ( 'NONE', *, *, #95666, .T. ) ;
#54588=ADVANCED_FACE ( 'NONE', ( #10402 ), #8242, .F. ) ;
#54589=VERTEX_POINT ( 'NONE', #32922 ) ;
#54591=CARTESIAN_POINT ( 'NONE',  ( -17.99451991528748351, 28.92564299267950645, 4.000000000000000000 ) ) ;
#54593=EDGE_LOOP ( 'NONE', ( #140138, #141733, #107081, #143390 ) ) ;
#54595=DIRECTION ( 'NONE',  ( -0.6830127018922180770, -0.6830127018922204085, -0.2588190451025213501 ) ) ;
#54596=EDGE_CURVE ( 'NONE', #18390, #128893, #53958, .T. ) ;
#54597=DIRECTION ( 'NONE',  ( -0.6830127018922181881, 0.6830127018922202975, -0.2588190451025214056 ) ) ;
#54599=ORIENTED_EDGE ( 'NONE', *, *, #103315, .F. ) ;
#54600=EDGE_CURVE ( 'NONE', #64063, #54084, #77144, .T. ) ;
#54601=CARTESIAN_POINT ( 'NONE',  ( -34.75611968250422024, 7.705650698523992759, 4.955485411084894487 ) ) ;
#54602=DIRECTION ( 'NONE',  ( -0.6830127018922180770, -0.6830127018922204085, -0.2588190451025213501 ) ) ;
#54603=FACE_OUTER_BOUND ( 'NONE', #106398, .T. ) ;
#54604=CARTESIAN_POINT ( 'NONE',  ( -66.29974487139159578, -27.71228299555252406, 4.000000000000000000 ) ) ;
#54605=LINE ( 'NONE', #98786, #83888 ) ;
#54606=FACE_OUTER_BOUND ( 'NONE', #30982, .T. ) ;
#54608=VECTOR ( 'NONE', #83084, 1000.000000000000227 ) ;
#54609=CARTESIAN_POINT ( 'NONE',  ( 20.56494995367816614, -2.598550695876024275, 5.000000000000000000 ) ) ;
#54611=ORIENTED_EDGE ( 'NONE', *, *, #4033, .T. ) ;
#54614=VECTOR ( 'NONE', #12539, 999.9999999999998863 ) ;
#54615=CARTESIAN_POINT ( 'NONE',  ( 27.48921356237309155, -27.52281430457074762, 5.000000000000000000 ) ) ;
#54616=PLANE ( 'NONE',  #34549 ) ;
#54617=ORIENTED_EDGE ( 'NONE', *, *, #18015, .F. ) ;
#54619=EDGE_CURVE ( 'NONE', #142915, #114801, #52488, .T. ) ;
#54620=CARTESIAN_POINT ( 'NONE',  ( -19.05000000000000071, 3.174999999999997158, 5.000000000000000000 ) ) ;
#54622=ORIENTED_EDGE ( 'NONE', *, *, #111222, .T. ) ;
#54624=ORIENTED_EDGE ( 'NONE', *, *, #39296, .F. ) ;
#54625=EDGE_LOOP ( 'NONE', ( #87885, #85019, #90843, #84316 ) ) ;
#54626=DIRECTION ( 'NONE',  ( -0.7071067811865486830, 0.7071067811865464625, 0.000000000000000000 ) ) ;
#54627=CARTESIAN_POINT ( 'NONE',  ( 12.29974487139158512, -27.71228299555214747, 4.000000000000000000 ) ) ;
#54628=PLANE ( 'NONE',  #4873 ) ;
#54629=DIRECTION ( 'NONE',  ( 0.7071067811865487940, 0.7071067811865463515, 0.000000000000000000 ) ) ;
#54631=DIRECTION ( 'NONE',  ( -0.000000000000000000, -0.3543493200069152693, 0.9351131265310292928 ) ) ;
#54633=VERTEX_POINT ( 'NONE', #142383 ) ;
#54639=AXIS2_PLACEMENT_3D ( 'NONE', #25723, #83717, #127921 ) ;
#54640=AXIS2_PLACEMENT_3D ( 'NONE', #122717, #13223, #69081 ) ;
#54641=EDGE_CURVE ( 'NONE', #57507, #82848, #43768, .T. ) ;
#54642=ORIENTED_EDGE ( 'NONE', *, *, #141730, .T. ) ;
#54644=CARTESIAN_POINT ( 'NONE',  ( -0.2997448713915885632, -27.71228299555206220, 4.000000000000000000 ) ) ;
#54646=EDGE_CURVE ( 'NONE', #37506, #13547, #21996, .T. ) ;
#54647=VECTOR ( 'NONE', #74775, 1000.000000000000227 ) ;
#54648=CARTESIAN_POINT ( 'NONE',  ( -8.277185695429338352, -21.72500000000000142, 5.000000000000000000 ) ) ;
#54649=DIRECTION ( 'NONE',  ( 0.7071067811865487940, 0.7071067811865463515, 0.000000000000000000 ) ) ;
#54650=CARTESIAN_POINT ( 'NONE',  ( 9.328169399223463998, -9.740707523384180888, 4.000000000000000000 ) ) ;
#54651=ORIENTED_EDGE ( 'NONE', *, *, #94554, .T. ) ;
#54652=VERTEX_POINT ( 'NONE', #11094 ) ;
#54653=CIRCLE ( 'NONE', #135671, 0.5000000000000000000 ) ;
#54655=CARTESIAN_POINT ( 'NONE',  ( 17.02886364525924989, -2.441401769420105339, 4.000000000000000000 ) ) ;
#54656=ORIENTED_EDGE ( 'NONE', *, *, #53732, .F. ) ;
#54657=EDGE_CURVE ( 'NONE', #16746, #143518, #97402, .T. ) ;
#54658=EDGE_CURVE ( 'NONE', #33564, #92017, #19858, .T. ) ;
#54659=ORIENTED_EDGE ( 'NONE', *, *, #23459, .F. ) ;
#54660=DIRECTION ( 'NONE',  ( -0.3543493200069162685, -0.000000000000000000, -0.9351131265310288487 ) ) ;
#54661=ORIENTED_EDGE ( 'NONE', *, *, #44972, .T. ) ;
#54662=CARTESIAN_POINT ( 'NONE',  ( 26.91508676806222411, -12.74070752338414536, 18.74364270924360198 ) ) ;
#54663=LINE ( 'NONE', #98846, #13195 ) ;
#54664=CARTESIAN_POINT ( 'NONE',  ( 20.68342038867197630, -6.740707523384219968, 11.88629033278119174 ) ) ;
#54665=ADVANCED_FACE ( 'NONE', ( #99546 ), #30769, .T. ) ;
#54666=FACE_BOUND ( 'NONE', #95170, .T. ) ;
#54668=CARTESIAN_POINT ( 'NONE',  ( 25.04515773336651208, -21.74070752338405654, 21.72585301388590295 ) ) ;
#54670=DIRECTION ( 'NONE',  ( -0.000000000000000000, 0.3543493200069153248, 0.9351131265310292928 ) ) ;
#54672=VERTEX_POINT ( 'NONE', #108261 ) ;
#54673=CARTESIAN_POINT ( 'NONE',  ( 75.48921356237309510, -27.52281430457107803, 5.000000000000000000 ) ) ;
#54676=ORIENTED_EDGE ( 'NONE', *, *, #14808, .F. ) ;
#54677=EDGE_LOOP ( 'NONE', ( #8446, #3847, #37235, #57498 ) ) ;
#54679=VERTEX_POINT ( 'NONE', #3779 ) ;
#54680=LINE ( 'NONE', #45950, #59218 ) ;
#54682=ORIENTED_EDGE ( 'NONE', *, *, #78201, .T. ) ;
#54683=DIRECTION ( 'NONE',  ( 0.7071067811865486830, -0.7071067811865464625, -0.000000000000000000 ) ) ;
#54684=ADVANCED_FACE ( 'NONE', ( #113286 ), #90862, .F. ) ;
#54685=CARTESIAN_POINT ( 'NONE',  ( -11.81601139373100651, 28.73617430169779041, 5.000000000000000000 ) ) ;
#54686=DIRECTION ( 'NONE',  ( 0.7071067811865487940, 0.7071067811865463515, 0.000000000000000000 ) ) ;
#54687=DIRECTION ( 'NONE',  ( 0.7071067811865487940, 0.7071067811865463515, 0.000000000000000000 ) ) ;
#54688=DIRECTION ( 'NONE',  ( -0.6830127018922180770, -0.6830127018922204085, -0.2588190451025213501 ) ) ;
#54689=CARTESIAN_POINT ( 'NONE',  ( -4.499999999999966249, -10.53360074219763298, 5.000000000000000000 ) ) ;
#54690=CARTESIAN_POINT ( 'NONE',  ( -14.81601139373099585, 28.73617430169776910, 5.000000000000000000 ) ) ;
#54691=CARTESIAN_POINT ( 'NONE',  ( 60.18398860626900415, 28.73617430169829490, 5.000000000000000000 ) ) ;
#54692=VERTEX_POINT ( 'NONE', #100297 ) ;
#54693=EDGE_CURVE ( 'NONE', #129495, #55173, #80692, .T. ) ;
#54695=EDGE_LOOP ( 'NONE', ( #100534, #63410, #42478, #12314 ) ) ;
#54696=CARTESIAN_POINT ( 'NONE',  ( 26.29289321881327623, 5.259292476615663681, 5.000000000000000000 ) ) ;
#54697=( BOUNDED_CURVE ( )  B_SPLINE_CURVE ( 3, ( #28632, #61975, #117038, #17704 ),
 .UNSPECIFIED., .F., .T. ) 
 B_SPLINE_CURVE_WITH_KNOTS ( ( 4, 4 ),
 ( 2.779374508378133601, 4.199602562396782091 ),
 .UNSPECIFIED. ) 
 CURVE ( )  GEOMETRIC_REPRESENTATION_ITEM ( )  RATIONAL_B_SPLINE_CURVE ( ( 1.000000000000000000, 0.8388583629366748173, 0.8388583629366748173, 1.000000000000000000 ) ) 
 REPRESENTATION_ITEM ( '' )  );
#54698=DIRECTION ( 'NONE',  ( 0.7071067811865486830, -0.7071067811865464625, -0.000000000000000000 ) ) ;
#54700=ORIENTED_EDGE ( 'NONE', *, *, #71175, .F. ) ;
#54701=EDGE_CURVE ( 'NONE', #27623, #39127, #56829, .T. ) ;
#54706=ADVANCED_FACE ( 'NONE', ( #123502 ), #3103, .F. ) ;
#54707=AXIS2_PLACEMENT_3D ( 'NONE', #116358, #38803, #137406 ) ;
#54711=ORIENTED_EDGE ( 'NONE', *, *, #99595, .F. ) ;
#54712=AXIS2_PLACEMENT_3D ( 'NONE', #26642, #49851, #71588 ) ;
#54713=CARTESIAN_POINT ( 'NONE',  ( -5.671830600776434750, 5.259292476615662792, 4.000000000000000000 ) ) ;
#54714=ORIENTED_EDGE ( 'NONE', *, *, #135034, .F. ) ;
#54716=DIRECTION ( 'NONE',  ( -0.7071067811865486830, 0.7071067811865464625, 0.000000000000000000 ) ) ;
#54717=CARTESIAN_POINT ( 'NONE',  ( 23.99451991528749062, 28.92564299267954908, 4.000000000000000000 ) ) ;
#54718=ORIENTED_EDGE ( 'NONE', *, *, #36069, .T. ) ;
#54719=ORIENTED_EDGE ( 'NONE', *, *, #28322, .F. ) ;
#54720=LINE ( 'NONE', #94084, #5560 ) ;
#54721=CARTESIAN_POINT ( 'NONE',  ( 31.49999999999977973, 10.08746187583915344, 4.000000000000000000 ) ) ;
#54722=DIRECTION ( 'NONE',  ( 0.7071067811865487940, -0.7071067811865463515, 0.000000000000000000 ) ) ;
#54723=VERTEX_POINT ( 'NONE', #134359 ) ;
#54724=LINE ( 'NONE', #43131, #143080 ) ;
#54725=ORIENTED_EDGE ( 'NONE', *, *, #72173, .F. ) ;
#54727=ADVANCED_FACE ( 'NONE', ( #35785 ), #35057, .F. ) ;
#54728=DIRECTION ( 'NONE',  ( -0.000000000000000000, 0.3543493200069153248, 0.9351131265310292928 ) ) ;
#54729=CARTESIAN_POINT ( 'NONE',  ( -23.67183060077630685, 14.25929247661557397, 4.000000000000000000 ) ) ;
#54730=DIRECTION ( 'NONE',  ( 0.7071067811865486830, -0.7071067811865464625, -0.000000000000000000 ) ) ;
#54731=CARTESIAN_POINT ( 'NONE',  ( -34.92500000000001137, 21.72500000000000142, 4.165035510187084178 ) ) ;
#54732=LINE ( 'NONE', #41698, #109885 ) ;
#54733=VECTOR ( 'NONE', #8558, 1000.000000000000000 ) ;
#54735=ORIENTED_EDGE ( 'NONE', *, *, #51404, .F. ) ;
#54736=EDGE_CURVE ( 'NONE', #33185, #93058, #45233, .T. ) ;
#54738=VERTEX_POINT ( 'NONE', #135773 ) ;
#54740=VECTOR ( 'NONE', #74239, 1000.000000000000000 ) ;
#54741=VECTOR ( 'NONE', #80856, 1000.000000000000000 ) ;
#54742=DIRECTION ( 'NONE',  ( 0.6830127018922181881, 0.6830127018922202975, -0.2588190451025214056 ) ) ;
#54743=DIRECTION ( 'NONE',  ( 0.000000000000000000, 1.000000000000000000, 0.000000000000000000 ) ) ;
#54744=VECTOR ( 'NONE', #71765, 1000.000000000000000 ) ;
#54745=EDGE_LOOP ( 'NONE', ( #80390, #57710, #115265 ) ) ;
#54747=CARTESIAN_POINT ( 'NONE',  ( -11.67183060077639567, 8.259292476615641476, 4.000000000000000000 ) ) ;
#54748=VERTEX_POINT ( 'NONE', #34316 ) ;
#54749=ORIENTED_EDGE ( 'NONE', *, *, #130710, .F. ) ;
#54750=DIRECTION ( 'NONE',  ( -0.000000000000000000, 0.000000000000000000, 1.000000000000000000 ) ) ;
#54751=CARTESIAN_POINT ( 'NONE',  ( 0.000000000000000000, 0.000000000000000000, 5.000000000000000000 ) ) ;
#54752=EDGE_CURVE ( 'NONE', #45511, #41681, #36463, .T. ) ;
#54755=CARTESIAN_POINT ( 'NONE',  ( -27.32816939922333077, 2.259292476615697876, 4.000000000000000000 ) ) ;
#54757=DIRECTION ( 'NONE',  ( 0.7071067811865487940, 0.7071067811865463515, -0.000000000000000000 ) ) ;
#54759=CARTESIAN_POINT ( 'NONE',  ( -66.29974487139159578, -27.71228299555252406, 4.000000000000000000 ) ) ;
#54760=DIRECTION ( 'NONE',  ( -0.000000000000000000, 0.3543493200069153248, 0.9351131265310292928 ) ) ;
#54761=EDGE_CURVE ( 'NONE', #86742, #83926, #124893, .T. ) ;
#54762=ORIENTED_EDGE ( 'NONE', *, *, #71866, .F. ) ;
#54763=LINE ( 'NONE', #130180, #134524 ) ;
#54764=ORIENTED_EDGE ( 'NONE', *, *, #136019, .F. ) ;
#54766=CARTESIAN_POINT ( 'NONE',  ( -34.49999999999975842, 21.05432934483072671, 4.994342998332167660 ) ) ;
#54768=DIRECTION ( 'NONE',  ( -0.000000000000000000, 0.3543493200069153248, 0.9351131265310292928 ) ) ;
#54769=LINE ( 'NONE', #1052, #57896 ) ;
#54770=ADVANCED_FACE ( 'NONE', ( #57520 ), #25567, .F. ) ;
#54771=DIRECTION ( 'NONE',  ( 0.7071067811865487940, 0.7071067811865463515, -0.000000000000000000 ) ) ;
#54773=ORIENTED_EDGE ( 'NONE', *, *, #16315, .F. ) ;
#54774=ADVANCED_FACE ( 'NONE', ( #67700 ), #4467, .F. ) ;
#54775=VERTEX_POINT ( 'NONE', #6624 ) ;
#54776=CARTESIAN_POINT ( 'NONE',  ( 32.99999999999976552, 7.931123077392109977, 4.000000000000000000 ) ) ;
#54779=CARTESIAN_POINT ( 'NONE',  ( 6.436801032208253837, -12.74070752338415247, 9.898150129686360543 ) ) ;
#54780=LINE ( 'NONE', #98957, #41136 ) ;
#54782=CARTESIAN_POINT ( 'NONE',  ( -34.92500000000001137, -10.19990548397269059, 4.759050581649336920 ) ) ;
#54783=VECTOR ( 'NONE', #74518, 1000.000000000000000 ) ;
#54784=CARTESIAN_POINT ( 'NONE',  ( -32.95560648933506798, 22.22500000000000142, 5.746276820986322420 ) ) ;
#54785=ORIENTED_EDGE ( 'NONE', *, *, #46483, .T. ) ;
#54787=EDGE_CURVE ( 'NONE', #46869, #115536, #18228, .T. ) ;
#54788=CARTESIAN_POINT ( 'NONE',  ( 0.000000000000000000, 0.000000000000000000, 5.000000000000000000 ) ) ;
#54789=LINE ( 'NONE', #109862, #71626 ) ;
#54791=VECTOR ( 'NONE', #93485, 1000.000000000000000 ) ;
#54792=ORIENTED_EDGE ( 'NONE', *, *, #512, .T. ) ;
#54793=EDGE_CURVE ( 'NONE', #103321, #89661, #16084, .T. ) ;
#54794=CARTESIAN_POINT ( 'NONE',  ( -27.18398860626900060, 28.73617430169806042, 5.000000000000000000 ) ) ;
#54795=ORIENTED_EDGE ( 'NONE', *, *, #49969, .F. ) ;
#54798=CARTESIAN_POINT ( 'NONE',  ( 18.79289321881332953, -20.24070752338407431, 5.000000000000000000 ) ) ;
#54799=EDGE_LOOP ( 'NONE', ( #33127, #61181, #66740 ) ) ;
#54801=CARTESIAN_POINT ( 'NONE',  ( -9.299744871391588674, -27.71228299555212971, 4.000000000000000000 ) ) ;
#54802=PLANE ( 'NONE',  #115938 ) ;
#54803=DIRECTION ( 'NONE',  ( -0.7071067811865486830, -0.7071067811865464625, -0.000000000000000000 ) ) ;
#54804=FACE_OUTER_BOUND ( 'NONE', #17936, .T. ) ;
#54805=PLANE ( 'NONE',  #98468 ) ;
#54806=ORIENTED_EDGE ( 'NONE', *, *, #101794, .F. ) ;
#54807=DIRECTION ( 'NONE',  ( 0.7071067811865487940, 0.7071067811865463515, -0.000000000000000000 ) ) ;
#54808=DIRECTION ( 'NONE',  ( 0.7071067811865487940, 0.7071067811865463515, 0.000000000000000000 ) ) ;
#54809=DIRECTION ( 'NONE',  ( 0.3543493200069162685, -0.000000000000000000, -0.9351131265310288487 ) ) ;
#54810=DIRECTION ( 'NONE',  ( 0.7071067811865487940, 0.7071067811865463515, 0.000000000000000000 ) ) ;
#54811=ORIENTED_EDGE ( 'NONE', *, *, #142379, .F. ) ;
#54812=VECTOR ( 'NONE', #53049, 1000.000000000000000 ) ;
#54813=EDGE_LOOP ( 'NONE', ( #39547, #86065, #75557, #107284 ) ) ;
#54815=EDGE_CURVE ( 'NONE', #138021, #86498, #7368, .T. ) ;
#54816=ORIENTED_EDGE ( 'NONE', *, *, #19179, .T. ) ;
#54818=PLANE ( 'NONE',  #93903 ) ;
#54819=EDGE_CURVE ( 'NONE', #12889, #94959, #62509, .T. ) ;
#54820=FACE_OUTER_BOUND ( 'NONE', #62268, .T. ) ;
#54822=FACE_OUTER_BOUND ( 'NONE', #91215, .T. ) ;
#54823=EDGE_LOOP ( 'NONE', ( #126469, #82650, #99852, #41320 ) ) ;
#54824=ORIENTED_EDGE ( 'NONE', *, *, #14548, .T. ) ;
#54825=DIRECTION ( 'NONE',  ( -0.000000000000000000, 0.000000000000000000, 1.000000000000000000 ) ) ;
#54827=ADVANCED_FACE ( 'NONE', ( #39330 ), #127013, .F. ) ;
#54829=ORIENTED_EDGE ( 'NONE', *, *, #26658, .F. ) ;
#54830=FACE_OUTER_BOUND ( 'NONE', #110258, .T. ) ;
#54831=DIRECTION ( 'NONE',  ( 1.000000000000000000, 0.000000000000000000, 0.000000000000000000 ) ) ;
#54832=DIRECTION ( 'NONE',  ( -0.7071067811865487940, 0.7071067811865463515, -0.000000000000000000 ) ) ;
#54833=EDGE_CURVE ( 'NONE', #77128, #88053, #83553, .T. ) ;
#54834=ORIENTED_EDGE ( 'NONE', *, *, #4622, .F. ) ;
#54835=VECTOR ( 'NONE', #38763, 1000.000000000000227 ) ;
#54837=FACE_BOUND ( 'NONE', #80564, .T. ) ;
#54841=DIRECTION ( 'NONE',  ( -0.7071067811865486830, -0.7071067811865464625, 0.000000000000000000 ) ) ;
#54842=VECTOR ( 'NONE', #40048, 1000.000000000000000 ) ;
#54844=DIRECTION ( 'NONE',  ( -0.000000000000000000, 0.000000000000000000, 1.000000000000000000 ) ) ;
#54846=ORIENTED_EDGE ( 'NONE', *, *, #122528, .T. ) ;
#54847=AXIS2_PLACEMENT_3D ( 'NONE', #10362, #12512, #67660 ) ;
#54849=EDGE_LOOP ( 'NONE', ( #105544, #56234, #11577, #135241 ) ) ;
#54852=ADVANCED_FACE ( 'NONE', ( #37168 ), #103814, .F. ) ;
#54853=ORIENTED_EDGE ( 'NONE', *, *, #43450, .F. ) ;
#54854=VECTOR ( 'NONE', #7512, 1000.000000000000000 ) ;
#54855=DIRECTION ( 'NONE',  ( -0.7071067811865486830, -0.7071067811865464625, 0.000000000000000000 ) ) ;
#54856=EDGE_CURVE ( 'NONE', #45976, #142614, #49516, .T. ) ;
#54857=LINE ( 'NONE', #19353, #66316 ) ;
#54858=CARTESIAN_POINT ( 'NONE',  ( -69.18398860626899705, 28.73617430169835529, 5.000000000000000000 ) ) ;
#54859=ORIENTED_EDGE ( 'NONE', *, *, #18719, .T. ) ;
#54861=PLANE ( 'NONE',  #33406 ) ;
#54863=CARTESIAN_POINT ( 'NONE',  ( -32.99999999999976552, -16.60178936734451582, 0.8616154019346735637 ) ) ;
#54864=FACE_OUTER_BOUND ( 'NONE', #115759, .T. ) ;
#54865=DIRECTION ( 'NONE',  ( -0.7071067811865486830, -0.7071067811865464625, 0.000000000000000000 ) ) ;
#54866=ADVANCED_FACE ( 'NONE', ( #60380 ), #94392, .F. ) ;
#54867=CARTESIAN_POINT ( 'NONE',  ( 32.99451991528749062, 28.92564299267960948, 4.000000000000000000 ) ) ;
#54869=DIRECTION ( 'NONE',  ( -0.7071067811865486830, -0.7071067811865464625, 0.000000000000000000 ) ) ;
#54870=CARTESIAN_POINT ( 'NONE',  ( -12.46160355370563799, -9.740707523384173783, 17.74957260769608069 ) ) ;
#54871=ORIENTED_EDGE ( 'NONE', *, *, #63681, .T. ) ;
#54872=ORIENTED_EDGE ( 'NONE', *, *, #17739, .F. ) ;
#54873=ORIENTED_EDGE ( 'NONE', *, *, #103611, .T. ) ;
#54876=EDGE_CURVE ( 'NONE', #89916, #89397, #129887, .T. ) ;
#54877=ORIENTED_EDGE ( 'NONE', *, *, #12746, .F. ) ;
#54879=CARTESIAN_POINT ( 'NONE',  ( -7.499999999999951150, 5.696342897626497148, -7.587980461218414518 ) ) ;
#54880=ADVANCED_FACE ( 'NONE', ( #54490 ), #21113, .F. ) ;
#54881=VECTOR ( 'NONE', #12708, 1000.000000000000000 ) ;
#54884=CARTESIAN_POINT ( 'NONE',  ( 20.99451991528748707, 28.92564299267952777, 4.000000000000000000 ) ) ;
#54885=VERTEX_POINT ( 'NONE', #42186 ) ;
#54886=CARTESIAN_POINT ( 'NONE',  ( -69.18398860626899705, 28.73617430169835529, 5.000000000000000000 ) ) ;
#54887=AXIS2_PLACEMENT_3D ( 'NONE', #78622, #90196, #122103 ) ;
#54888=ADVANCED_FACE ( 'NONE', ( #41436 ), #131315, .F. ) ;
#54889=FACE_OUTER_BOUND ( 'NONE', #105634, .T. ) ;
#54891=DIRECTION ( 'NONE',  ( -0.3543493200069163240, 0.000000000000000000, -0.9351131265310288487 ) ) ;
#54892=ORIENTED_EDGE ( 'NONE', *, *, #56191, .F. ) ;
#54895=EDGE_LOOP ( 'NONE', ( #102844, #77550, #48683, #134276 ) ) ;
#54898=VECTOR ( 'NONE', #61739, 1000.000000000000000 ) ;
#54900=CARTESIAN_POINT ( 'NONE',  ( 60.18398860626900415, 28.73617430169829490, 5.000000000000000000 ) ) ;
#54901=VECTOR ( 'NONE', #105965, 1000.000000000000000 ) ;
#54902=CARTESIAN_POINT ( 'NONE',  ( -2.816011393730999401, 28.73617430169785436, 5.000000000000000000 ) ) ;
#54905=LINE ( 'NONE', #9941, #104416 ) ;
#54908=CARTESIAN_POINT ( 'NONE',  ( 15.18398860626900237, 28.73617430169797871, 5.000000000000000000 ) ) ;
#54909=CARTESIAN_POINT ( 'NONE',  ( 20.99451991528748707, 28.92564299267952777, 4.000000000000000000 ) ) ;
#54910=VECTOR ( 'NONE', #49521, 999.9999999999998863 ) ;
#54912=VERTEX_POINT ( 'NONE', #130628 ) ;
#54913=VERTEX_POINT ( 'NONE', #29838 ) ;
#54914=EDGE_CURVE ( 'NONE', #111735, #19820, #31997, .T. ) ;
#54915=EDGE_LOOP ( 'NONE', ( #37940, #27040, #101141, #89871, #19210 ) ) ;
#54917=FACE_OUTER_BOUND ( 'NONE', #10398, .T. ) ;
#54919=CARTESIAN_POINT ( 'NONE',  ( -30.48921356237309510, -27.52281430457076894, 5.000000000000000000 ) ) ;
#54920=CARTESIAN_POINT ( 'NONE',  ( 7.499999999999947597, 21.43112307739195899, 4.000000000000000000 ) ) ;
#54923=DIRECTION ( 'NONE',  ( 0.7071067811865487940, 0.7071067811865463515, -0.000000000000000000 ) ) ;
#54924=LINE ( 'NONE', #100568, #4921 ) ;
#54925=VERTEX_POINT ( 'NONE', #121134 ) ;
#54926=CARTESIAN_POINT ( 'NONE',  ( -22.17183060077631396, -8.240707523384200428, 4.000000000000000000 ) ) ;
#54927=ORIENTED_EDGE ( 'NONE', *, *, #36454, .T. ) ;
#54929=ORIENTED_EDGE ( 'NONE', *, *, #9064, .T. ) ;
#54930=DIRECTION ( 'NONE',  ( -0.000000000000000000, -0.3543493200069152693, 0.9351131265310292928 ) ) ;
#54931=PLANE ( 'NONE',  #7041 ) ;
#54932=ORIENTED_EDGE ( 'NONE', *, *, #16812, .T. ) ;
#54933=VECTOR ( 'NONE', #116678, 1000.000000000000000 ) ;
#54935=DIRECTION ( 'NONE',  ( 0.6830127018922181881, 0.6830127018922202975, -0.2588190451025214056 ) ) ;
#54937=CARTESIAN_POINT ( 'NONE',  ( -3.792893218813429002, -20.24070752338408141, 5.000000000000000000 ) ) ;
#54939=PLANE ( 'NONE',  #37419 ) ;
#54940=ORIENTED_EDGE ( 'NONE', *, *, #97338, .F. ) ;
#54941=AXIS2_PLACEMENT_3D ( 'NONE', #130074, #84446, #131499 ) ;
#54943=VECTOR ( 'NONE', #111836, 1000.000000000000114 ) ;
#54944=ADVANCED_FACE ( 'NONE', ( #120390 ), #96505, .F. ) ;
#54945=EDGE_CURVE ( 'NONE', #46130, #125641, #98669, .T. ) ;
#54946=DIRECTION ( 'NONE',  ( 0.7071067811865487940, 0.7071067811865463515, 0.000000000000000000 ) ) ;
#54947=VECTOR ( 'NONE', #94360, 1000.000000000000000 ) ;
#54949=CARTESIAN_POINT ( 'NONE',  ( 14.99999999999989875, 7.931123077392104648, 4.000000000000000000 ) ) ;
#54950=LINE ( 'NONE', #54257, #13511 ) ;
#54959=DIRECTION ( 'NONE',  ( 0.7071067811865486830, -0.7071067811865464625, -0.000000000000000000 ) ) ;
#54960=VERTEX_POINT ( 'NONE', #119003 ) ;
#54961=EDGE_LOOP ( 'NONE', ( #137447, #53999, #107585, #105954 ) ) ;
#54962=ADVANCED_FACE ( 'NONE', ( #55191 ), #87799, .F. ) ;
#54963=CARTESIAN_POINT ( 'NONE',  ( 45.29974487139158867, -27.71228299555237840, 4.000000000000000000 ) ) ;
#54965=CARTESIAN_POINT ( 'NONE',  ( 0.4892135623730947680, -27.52281430457055578, 5.000000000000000000 ) ) ;
#54966=CARTESIAN_POINT ( 'NONE',  ( -4.499999999999964473, 15.43112307739203004, 4.000000000000000000 ) ) ;
#54968=ORIENTED_EDGE ( 'NONE', *, *, #122030, .T. ) ;
#54969=ADVANCED_FACE ( 'NONE', ( #108098 ), #76967, .F. ) ;
#54972=CARTESIAN_POINT ( 'NONE',  ( -5.999999999999958256, 13.93112307739204603, 4.000000000000000000 ) ) ;
#54973=CARTESIAN_POINT ( 'NONE',  ( -48.29974487139158867, -27.71228299555239971, 4.000000000000000000 ) ) ;
#54974=CARTESIAN_POINT ( 'NONE',  ( 14.99999999999990052, 10.93112307739207445, 4.000000000000000000 ) ) ;
#54975=LINE ( 'NONE', #111472, #5720 ) ;
#54976=VERTEX_POINT ( 'NONE', #108811 ) ;
#54977=DIRECTION ( 'NONE',  ( 0.7071067811865486830, -0.7071067811865464625, -0.000000000000000000 ) ) ;
#54982=DIRECTION ( 'NONE',  ( 0.7071067811865486830, -0.7071067811865464625, -0.000000000000000000 ) ) ;
#54983=CARTESIAN_POINT ( 'NONE',  ( 5.510786437626906675, -27.52281430457051314, 5.000000000000000000 ) ) ;
#54985=ORIENTED_EDGE ( 'NONE', *, *, #65477, .T. ) ;
#54986=ORIENTED_EDGE ( 'NONE', *, *, #6004, .T. ) ;
#54988=AXIS2_PLACEMENT_3D ( 'NONE', #31727, #41164, #30293 ) ;
#54989=VERTEX_POINT ( 'NONE', #10923 ) ;
#54991=CARTESIAN_POINT ( 'NONE',  ( 14.99451991528749595, 28.92564299267948513, 4.000000000000000000 ) ) ;
#54992=VECTOR ( 'NONE', #23594, 1000.000000000000000 ) ;
#54993=CARTESIAN_POINT ( 'NONE',  ( -26.67183060077628198, -9.740707523384187994, 4.000000000000000000 ) ) ;
#54994=EDGE_LOOP ( 'NONE', ( #94955, #53118, #31821, #107779 ) ) ;
#54997=ADVANCED_FACE ( 'NONE', ( #66776 ), #22515, .F. ) ;
#54998=EDGE_CURVE ( 'NONE', #28039, #24388, #110948, .T. ) ;
#55000=ORIENTED_EDGE ( 'NONE', *, *, #71779, .F. ) ;
#55002=VECTOR ( 'NONE', #2118, 1000.000000000000227 ) ;
#55003=CARTESIAN_POINT ( 'NONE',  ( 11.91508676806230582, -12.74070752338415602, 18.74364270924357001 ) ) ;
#55004=EDGE_CURVE ( 'NONE', #66852, #98615, #121833, .T. ) ;
#55005=VERTEX_POINT ( 'NONE', #1474 ) ;
#55006=ORIENTED_EDGE ( 'NONE', *, *, #75247, .F. ) ;
#55008=EDGE_LOOP ( 'NONE', ( #108280, #138800, #56601, #28226 ) ) ;
#55009=LINE ( 'NONE', #110061, #28299 ) ;
#55010=EDGE_CURVE ( 'NONE', #129972, #103979, #91398, .T. ) ;
#55011=LINE ( 'NONE', #589, #43227 ) ;
#55013=CARTESIAN_POINT ( 'NONE',  ( 0.000000000000000000, 0.000000000000000000, 5.000000000000000000 ) ) ;
#55015=DIRECTION ( 'NONE',  ( 0.7071067811865486830, -0.7071067811865464625, -0.000000000000000000 ) ) ;
#55018=ORIENTED_EDGE ( 'NONE', *, *, #5365, .F. ) ;
#55020=CARTESIAN_POINT ( 'NONE',  ( 16.21321903303349643, 12.75929247661559351, 10.29404684609039045 ) ) ;
#55021=VERTEX_POINT ( 'NONE', #11636 ) ;
#55022=ORIENTED_EDGE ( 'NONE', *, *, #88392, .F. ) ;
#55023=EDGE_CURVE ( 'NONE', #49119, #143446, #112420, .T. ) ;
#55024=VECTOR ( 'NONE', #46800, 1000.000000000000000 ) ;
#55025=DIRECTION ( 'NONE',  ( 0.7071067811865486830, -0.7071067811865464625, -0.000000000000000000 ) ) ;
#55026=ORIENTED_EDGE ( 'NONE', *, *, #3860, .F. ) ;
#55027=DIRECTION ( 'NONE',  ( -0.000000000000000000, 0.3543493200069153248, 0.9351131265310292928 ) ) ;
#55028=CARTESIAN_POINT ( 'NONE',  ( 13.49999999999990408, -20.53675388469229546, 2.352720554255925300 ) ) ;
#55029=CARTESIAN_POINT ( 'NONE',  ( -12.48921356237309155, -27.52281430457064104, 5.000000000000000000 ) ) ;
#55030=FACE_OUTER_BOUND ( 'NONE', #125830, .T. ) ;
#55031=DIRECTION ( 'NONE',  ( 1.000000000000000000, 0.000000000000000000, 0.000000000000000000 ) ) ;
#55032=ORIENTED_EDGE ( 'NONE', *, *, #73202, .F. ) ;
#55033=CARTESIAN_POINT ( 'NONE',  ( 25.37176554955600238, -8.240707523384196875, 11.38925528200746662 ) ) ;
#55034=AXIS2_PLACEMENT_3D ( 'NONE', #16452, #118647, #5585 ) ;
#55035=VERTEX_POINT ( 'NONE', #45066 ) ;
#55037=ORIENTED_EDGE ( 'NONE', *, *, #19563, .F. ) ;
#55039=VERTEX_POINT ( 'NONE', #13777 ) ;
#55040=DIRECTION ( 'NONE',  ( -0.7071067811865486830, -0.7071067811865464625, 0.000000000000000000 ) ) ;
#55042=ORIENTED_EDGE ( 'NONE', *, *, #47644, .F. ) ;
#55043=AXIS2_PLACEMENT_3D ( 'NONE', #112960, #123153, #23824 ) ;
#55045=VECTOR ( 'NONE', #118289, 1000.000000000000000 ) ;
#55046=EDGE_CURVE ( 'NONE', #75268, #16508, #101525, .T. ) ;
#55047=DIRECTION ( 'NONE',  ( -0.7071067811865486830, -0.7071067811865464625, 0.000000000000000000 ) ) ;
#55048=CARTESIAN_POINT ( 'NONE',  ( 22.82900182742193351, 7.795401085224272109, 5.000000000000000000 ) ) ;
#55049=CARTESIAN_POINT ( 'NONE',  ( 0.4892135623730947680, -27.52281430457055578, 5.000000000000000000 ) ) ;
#55050=DIRECTION ( 'NONE',  ( 0.6830127018922181881, 0.6830127018922202975, -0.2588190451025214056 ) ) ;
#55051=DIRECTION ( 'NONE',  ( -0.6830127018922181881, 0.6830127018922202975, -0.2588190451025214056 ) ) ;
#55053=CARTESIAN_POINT ( 'NONE',  ( -25.26506670282035927, 12.75929247661558286, 18.34774599283961649 ) ) ;
#55054=DIRECTION ( 'NONE',  ( -0.7071067811865486830, -0.7071067811865464625, 0.000000000000000000 ) ) ;
#55055=VECTOR ( 'NONE', #1797, 1000.000000000000000 ) ;
#55056=DIRECTION ( 'NONE',  ( 0.7071067811865486830, -0.7071067811865464625, -0.000000000000000000 ) ) ;
#55058=PLANE ( 'NONE',  #55240 ) ;
#55059=LINE ( 'NONE', #90541, #137475 ) ;
#55060=ORIENTED_EDGE ( 'NONE', *, *, #80011, .F. ) ;
#55061=VERTEX_POINT ( 'NONE', #36291 ) ;
#55062=ORIENTED_EDGE ( 'NONE', *, *, #28891, .T. ) ;
#55064=EDGE_LOOP ( 'NONE', ( #4684, #136486, #53637, #51771 ) ) ;
#55065=ORIENTED_EDGE ( 'NONE', *, *, #125704, .T. ) ;
#55066=CARTESIAN_POINT ( 'NONE',  ( -23.34505516254603208, 5.259292476615669010, 12.77922209995888458 ) ) ;
#55067=FACE_OUTER_BOUND ( 'NONE', #103496, .T. ) ;
#55068=DIRECTION ( 'NONE',  ( -0.000000000000000000, 0.3543493200069153248, 0.9351131265310292928 ) ) ;
#55069=CARTESIAN_POINT ( 'NONE',  ( 0.4892135623730947680, -27.52281430457055578, 5.000000000000000000 ) ) ;
#55070=DIRECTION ( 'NONE',  ( 0.7071067811865486830, -0.7071067811865464625, -0.000000000000000000 ) ) ;
#55071=ORIENTED_EDGE ( 'NONE', *, *, #136141, .F. ) ;
#55073=CARTESIAN_POINT ( 'NONE',  ( 36.18398860626899705, 28.73617430169812437, 5.000000000000000000 ) ) ;
#55074=ORIENTED_EDGE ( 'NONE', *, *, #136320, .F. ) ;
#55075=DIRECTION ( 'NONE',  ( 0.6830127018922181881, 0.6830127018922202975, -0.2588190451025214056 ) ) ;
#55077=ORIENTED_EDGE ( 'NONE', *, *, #124438, .F. ) ;
#55079=LINE ( 'NONE', #97861, #117684 ) ;
#55080=CARTESIAN_POINT ( 'NONE',  ( -16.49999999999987921, -20.56887692260760758, 4.000000000000000000 ) ) ;
#55082=ORIENTED_EDGE ( 'NONE', *, *, #132060, .T. ) ;
#55083=EDGE_LOOP ( 'NONE', ( #127895, #103251, #100531, #67059, #117483 ) ) ;
#55084=PLANE ( 'NONE',  #33378 ) ;
#55085=CARTESIAN_POINT ( 'NONE',  ( 22.49999999999985434, 22.22500000000000142, 4.362957392718788796 ) ) ;
#55086=CARTESIAN_POINT ( 'NONE',  ( 66.18398860626901126, 28.73617430169833753, 5.000000000000000000 ) ) ;
#55087=CARTESIAN_POINT ( 'NONE',  ( 14.67183060077636725, 17.25929247661554200, 4.000000000000000000 ) ) ;
#55088=CARTESIAN_POINT ( 'NONE',  ( 11.51078643762690490, -27.52281430457047406, 5.000000000000000000 ) ) ;
#55089=ORIENTED_EDGE ( 'NONE', *, *, #142889, .T. ) ;
#55090=LINE ( 'NONE', #42084, #62269 ) ;
#55091=CARTESIAN_POINT ( 'NONE',  ( 34.49999999999975842, -10.53574439159940113, 4.994342998332163219 ) ) ;
#55092=DIRECTION ( 'NONE',  ( 0.7071067811865487940, 0.7071067811865463515, 0.000000000000000000 ) ) ;
#55094=EDGE_CURVE ( 'NONE', #90647, #118382, #132777, .T. ) ;
#55095=ORIENTED_EDGE ( 'NONE', *, *, #102902, .F. ) ;
#55096=DIRECTION ( 'NONE',  ( -0.7071067811865486830, -0.7071067811865464625, 0.000000000000000000 ) ) ;
#55097=DIRECTION ( 'NONE',  ( 0.7071067811865487940, -0.7071067811865463515, 0.000000000000000000 ) ) ;
#55098=ORIENTED_EDGE ( 'NONE', *, *, #110633, .T. ) ;
#55102=ORIENTED_EDGE ( 'NONE', *, *, #72000, .T. ) ;
#55103=EDGE_CURVE ( 'NONE', #69963, #99168, #68940, .T. ) ;
#55105=FACE_OUTER_BOUND ( 'NONE', #68334, .T. ) ;
#55106=PLANE ( 'NONE',  #99296 ) ;
#55108=DIRECTION ( 'NONE',  ( -0.6830127018922180770, -0.6830127018922204085, -0.2588190451025214056 ) ) ;
#55110=EDGE_CURVE ( 'NONE', #128780, #75355, #122555, .T. ) ;
#55112=CARTESIAN_POINT ( 'NONE',  ( 69.18398860626899705, 28.73617430169835529, 5.000000000000000000 ) ) ;
#55113=CARTESIAN_POINT ( 'NONE',  ( 20.99451991528748707, 28.92564299267952777, 4.000000000000000000 ) ) ;
#55114=CARTESIAN_POINT ( 'NONE',  ( -7.499999999999944045, -2.568876922607786550, 4.000000000000000000 ) ) ;
#55116=DIRECTION ( 'NONE',  ( -0.3543493200069162685, -0.000000000000000000, -0.9351131265310288487 ) ) ;
#55117=CARTESIAN_POINT ( 'NONE',  ( 17.14818355038134712, 17.25929247661554555, 8.802941693769241738 ) ) ;
#55118=CARTESIAN_POINT ( 'NONE',  ( -25.49999999999982592, 12.43112307739206024, 4.000000000000000000 ) ) ;
#55119=CARTESIAN_POINT ( 'NONE',  ( 18.18398860626898994, 28.73617430169800002, 5.000000000000000000 ) ) ;
#55120=LINE ( 'NONE', #32656, #113963 ) ;
#55121=DIRECTION ( 'NONE',  ( 0.7071067811865487940, 0.7071067811865463515, -0.000000000000000000 ) ) ;
#55122=DIRECTION ( 'NONE',  ( -0.7071067811865486830, 0.7071067811865463515, 0.000000000000000000 ) ) ;
#55123=DIRECTION ( 'NONE',  ( 0.000000000000000000, 0.000000000000000000, 1.000000000000000000 ) ) ;
#55124=VERTEX_POINT ( 'NONE', #57350 ) ;
#55125=VERTEX_POINT ( 'NONE', #2175 ) ;
#55128=ORIENTED_EDGE ( 'NONE', *, *, #133066, .T. ) ;
#55129=ORIENTED_EDGE ( 'NONE', *, *, #32683, .T. ) ;
#55130=ORIENTED_EDGE ( 'NONE', *, *, #106042, .T. ) ;
#55133=ORIENTED_EDGE ( 'NONE', *, *, #132747, .T. ) ;
#55135=DIRECTION ( 'NONE',  ( -0.7071067811865487940, 0.7071067811865463515, -0.000000000000000000 ) ) ;
#55136=CARTESIAN_POINT ( 'NONE',  ( 16.22674160717823355, -11.24070752338416490, 18.24660765846986266 ) ) ;
#55138=CARTESIAN_POINT ( 'NONE',  ( 74.99451991528749772, 28.92564299267990435, 4.000000000000000000 ) ) ;
#55139=CARTESIAN_POINT ( 'NONE',  ( 34.92499999999998295, -21.72500000000000142, 5.000000000000000000 ) ) ;
#55140=VERTEX_POINT ( 'NONE', #79838 ) ;
#55141=CARTESIAN_POINT ( 'NONE',  ( 63.18398860626900415, 28.73617430169831621, 5.000000000000000000 ) ) ;
#55142=CARTESIAN_POINT ( 'NONE',  ( -10.49999999999992539, 16.18958161055401490, -11.56426086740813730 ) ) ;
#55143=CARTESIAN_POINT ( 'NONE',  ( 33.48921356237309510, -27.52281430457078670, 5.000000000000000000 ) ) ;
#55144=EDGE_CURVE ( 'NONE', #66817, #88412, #94918, .T. ) ;
#55145=VECTOR ( 'NONE', #142934, 1000.000000000000000 ) ;
#55146=CARTESIAN_POINT ( 'NONE',  ( 15.70710678118643777, -18.74070752338409562, 5.000000000000000000 ) ) ;
#55147=LINE ( 'NONE', #77623, #12116 ) ;
#55148=CARTESIAN_POINT ( 'NONE',  ( 10.49999999999993605, -4.912538124160710673, 4.000000000000000000 ) ) ;
#55149=VECTOR ( 'NONE', #73227, 999.9999999999998863 ) ;
#55150=DIRECTION ( 'NONE',  ( 0.7071067811865486830, -0.7071067811865464625, -0.000000000000000000 ) ) ;
#55151=CARTESIAN_POINT ( 'NONE',  ( 32.99451991528749062, 28.92564299267960948, 4.000000000000000000 ) ) ;
#55152=ORIENTED_EDGE ( 'NONE', *, *, #126470, .F. ) ;
#55153=ORIENTED_EDGE ( 'NONE', *, *, #5976, .T. ) ;
#55156=CARTESIAN_POINT ( 'NONE',  ( 34.92499999999998295, -16.19990548397266039, 4.759050581649326261 ) ) ;
#55157=ADVANCED_FACE ( 'NONE', ( #61631 ), #5033, .F. ) ;
#55158=CARTESIAN_POINT ( 'NONE',  ( 19.63753812416084443, 22.22500000000000142, 4.000000000000000000 ) ) ;
#55159=LINE ( 'NONE', #99338, #8613 ) ;
#55160=LINE ( 'NONE', #45734, #67510 ) ;
#55162=EDGE_CURVE ( 'NONE', #2927, #89784, #105097, .T. ) ;
#55164=ORIENTED_EDGE ( 'NONE', *, *, #43658, .F. ) ;
#55165=EDGE_CURVE ( 'NONE', #54738, #128151, #127574, .T. ) ;
#55166=ORIENTED_EDGE ( 'NONE', *, *, #142549, .T. ) ;
#55167=CARTESIAN_POINT ( 'NONE',  ( 23.27718569542924243, -21.72500000000000142, 5.000000000000000000 ) ) ;
#55168=FACE_OUTER_BOUND ( 'NONE', #106513, .T. ) ;
#55169=EDGE_CURVE ( 'NONE', #99905, #125583, #82648, .T. ) ;
#55170=VECTOR ( 'NONE', #1029, 1000.000000000000227 ) ;
#55172=ORIENTED_EDGE ( 'NONE', *, *, #102350, .F. ) ;
#55173=VERTEX_POINT ( 'NONE', #117373 ) ;
#55175=ORIENTED_EDGE ( 'NONE', *, *, #30775, .T. ) ;
#55176=CARTESIAN_POINT ( 'NONE',  ( 8.999999999999937828, -2.904428200921304271, -6.989807076074965764 ) ) ;
#55177=CARTESIAN_POINT ( 'NONE',  ( 69.29974487139159578, -27.71228299555254537, 4.000000000000000000 ) ) ;
#55178=VECTOR ( 'NONE', #12229, 1000.000000000000000 ) ;
#55180=ADVANCED_FACE ( 'NONE', ( #26824 ), #4288, .T. ) ;
#55182=VERTEX_POINT ( 'NONE', #73210 ) ;
#55183=EDGE_CURVE ( 'NONE', #132937, #20628, #71075, .T. ) ;
#55184=CARTESIAN_POINT ( 'NONE',  ( -2.953411863704541673, 14.25929247661557753, 18.84478104361328832 ) ) ;
#55185=ORIENTED_EDGE ( 'NONE', *, *, #89250, .T. ) ;
#55186=ORIENTED_EDGE ( 'NONE', *, *, #3778, .F. ) ;
#55188=ORIENTED_EDGE ( 'NONE', *, *, #125262, .F. ) ;
#55191=FACE_OUTER_BOUND ( 'NONE', #100553, .T. ) ;
#55192=EDGE_CURVE ( 'NONE', #58171, #126408, #137752, .T. ) ;
#55194=FACE_OUTER_BOUND ( 'NONE', #53656, .T. ) ;
#55195=PLANE ( 'NONE',  #117788 ) ;
#55197=EDGE_CURVE ( 'NONE', #124072, #123554, #58809, .T. ) ;
#55198=FACE_BOUND ( 'NONE', #133958, .T. ) ;
#55199=ORIENTED_EDGE ( 'NONE', *, *, #132201, .T. ) ;
#55200=FACE_OUTER_BOUND ( 'NONE', #141503, .T. ) ;
#55202=DIRECTION ( 'NONE',  ( -0.000000000000000000, 0.000000000000000000, 1.000000000000000000 ) ) ;
#55203=VERTEX_POINT ( 'NONE', #103644 ) ;
#55204=DIRECTION ( 'NONE',  ( 0.7071067811865487940, 0.7071067811865463515, -0.000000000000000000 ) ) ;
#55205=ORIENTED_EDGE ( 'NONE', *, *, #108009, .T. ) ;
#55206=EDGE_LOOP ( 'NONE', ( #26641, #87317, #30096, #34951 ) ) ;
#55207=VERTEX_POINT ( 'NONE', #39144 ) ;
#55209=EDGE_LOOP ( 'NONE', ( #50267, #94370, #82688, #101934 ) ) ;
#55210=LINE ( 'NONE', #129907, #51011 ) ;
#55211=CARTESIAN_POINT ( 'NONE',  ( 11.67183060077638856, 17.25929247661554555, 4.000000000000000000 ) ) ;
#55212=CARTESIAN_POINT ( 'NONE',  ( 45.48921356237309510, -27.52281430457087197, 5.000000000000000000 ) ) ;
#55214=CARTESIAN_POINT ( 'NONE',  ( 34.49999999999976552, -4.535744391599457082, 4.994342998332164107 ) ) ;
#55215=CARTESIAN_POINT ( 'NONE',  ( 20.99451991528748707, 28.92564299267952777, 4.000000000000000000 ) ) ;
#55216=EDGE_CURVE ( 'NONE', #107904, #138649, #38429, .T. ) ;
#55217=EDGE_CURVE ( 'NONE', #76456, #114150, #27523, .T. ) ;
#55219=DIRECTION ( 'NONE',  ( -0.7071067811865486830, 0.7071067811865464625, 0.000000000000000000 ) ) ;
#55220=CARTESIAN_POINT ( 'NONE',  ( -16.49999999999988276, -6.839392718269142080, -8.480912228396045194 ) ) ;
#55221=DIRECTION ( 'NONE',  ( -0.7071067811865486830, -0.7071067811865464625, 0.000000000000000000 ) ) ;
#55222=DIRECTION ( 'NONE',  ( -0.000000000000000000, 0.3543493200069153248, 0.9351131265310292928 ) ) ;
#55223=ORIENTED_EDGE ( 'NONE', *, *, #102951, .T. ) ;
#55226=LINE ( 'NONE', #57385, #28831 ) ;
#55227=VECTOR ( 'NONE', #47057, 1000.000000000000000 ) ;
#55228=LINE ( 'NONE', #11676, #93079 ) ;
#55229=ORIENTED_EDGE ( 'NONE', *, *, #76961, .F. ) ;
#55230=VECTOR ( 'NONE', #82837, 1000.000000000000000 ) ;
#55231=AXIS2_PLACEMENT_3D ( 'NONE', #99019, #87463, #66428 ) ;
#55232=ORIENTED_EDGE ( 'NONE', *, *, #103146, .T. ) ;
#55234=DIRECTION ( 'NONE',  ( 0.7071067811865487940, 0.7071067811865463515, -0.000000000000000000 ) ) ;
#55235=EDGE_CURVE ( 'NONE', #44871, #93122, #102974, .T. ) ;
#55236=VECTOR ( 'NONE', #110672, 1000.000000000000000 ) ;
#55237=CARTESIAN_POINT ( 'NONE',  ( 27.48921356237309155, -27.52281430457074762, 5.000000000000000000 ) ) ;
#55238=ORIENTED_EDGE ( 'NONE', *, *, #13014, .F. ) ;
#55239=DIRECTION ( 'NONE',  ( -0.000000000000000000, -0.3543493200069152693, 0.9351131265310292928 ) ) ;
#55240=AXIS2_PLACEMENT_3D ( 'NONE', #76827, #121001, #74678 ) ;
#55241=VECTOR ( 'NONE', #67795, 1000.000000000000000 ) ;
#55242=CARTESIAN_POINT ( 'NONE',  ( 19.49999999999986500, -9.462702396500995761, -9.474982329943561155 ) ) ;
#55244=DIRECTION ( 'NONE',  ( -0.7071067811865486830, -0.7071067811865464625, -0.000000000000000000 ) ) ;
#55245=VERTEX_POINT ( 'NONE', #115953 ) ;
#55248=PLANE ( 'NONE',  #76664 ) ;
#55249=CARTESIAN_POINT ( 'NONE',  ( 19.49999999999985789, 5.696342897626518464, -7.587980461218352346 ) ) ;
#55251=ORIENTED_EDGE ( 'NONE', *, *, #52564, .F. ) ;
#55254=ORIENTED_EDGE ( 'NONE', *, *, #123469, .F. ) ;
#55255=PLANE ( 'NONE',  #49693 ) ;
#55256=CARTESIAN_POINT ( 'NONE',  ( 24.83652871126534123, 15.75929247661555443, 9.299976744542977514 ) ) ;
#55257=DIRECTION ( 'NONE',  ( -0.3543493200069162685, -0.000000000000000000, -0.9351131265310288487 ) ) ;
#55258=ORIENTED_EDGE ( 'NONE', *, *, #26850, .F. ) ;
#55259=VECTOR ( 'NONE', #29428, 1000.000000000000000 ) ;
#55260=EDGE_CURVE ( 'NONE', #117635, #84441, #83361, .T. ) ;
#55261=CARTESIAN_POINT ( 'NONE',  ( 0.4892135623730947680, -27.52281430457055578, 5.000000000000000000 ) ) ;
#55262=PLANE ( 'NONE',  #72303 ) ;
#55263=ORIENTED_EDGE ( 'NONE', *, *, #27776, .T. ) ;
#55264=ADVANCED_FACE ( 'NONE', ( #5760 ), #50026, .F. ) ;
#55265=LINE ( 'NONE', #88618, #64762 ) ;
#55266=LINE ( 'NONE', #33538, #97826 ) ;
#55267=VECTOR ( 'NONE', #58547, 1000.000000000000000 ) ;
#55268=ORIENTED_EDGE ( 'NONE', *, *, #7924, .T. ) ;
#55270=DIRECTION ( 'NONE',  ( -0.6830127018922181881, 0.6830127018922202975, -0.2588190451025214056 ) ) ;
#55272=ORIENTED_EDGE ( 'NONE', *, *, #94668, .T. ) ;
#55273=ADVANCED_FACE ( 'NONE', ( #36979 ), #138455, .F. ) ;
#55274=ORIENTED_EDGE ( 'NONE', *, *, #99471, .F. ) ;
#55276=VECTOR ( 'NONE', #126087, 1000.000000000000000 ) ;
#55277=LINE ( 'NONE', #99453, #94549 ) ;
#55278=ORIENTED_EDGE ( 'NONE', *, *, #102518, .T. ) ;
#55279=VECTOR ( 'NONE', #7203, 1000.000000000000000 ) ;
#55281=EDGE_CURVE ( 'NONE', #46561, #106533, #81965, .T. ) ;
#55282=EDGE_CURVE ( 'NONE', #10669, #95640, #85469, .T. ) ;
#55283=LINE ( 'NONE', #129980, #50681 ) ;
#55284=LINE ( 'NONE', #23333, #42181 ) ;
#55285=ADVANCED_FACE ( 'NONE', ( #96326 ), #118079, .T. ) ;
#55286=EDGE_LOOP ( 'NONE', ( #141890, #70780, #116974, #68941 ) ) ;
#55287=DIRECTION ( 'NONE',  ( 1.000000000000000000, 0.000000000000000000, 0.000000000000000000 ) ) ;
#55288=EDGE_CURVE ( 'NONE', #65140, #91460, #33812, .T. ) ;
#55289=CARTESIAN_POINT ( 'NONE',  ( 42.18398860626899705, 28.73617430169816700, 5.000000000000000000 ) ) ;
#55291=VECTOR ( 'NONE', #114094, 1000.000000000000227 ) ;
#55293=ADVANCED_FACE ( 'NONE', ( #78031 ), #100492, .T. ) ;
#55295=CARTESIAN_POINT ( 'NONE',  ( -33.18398860626899705, 28.73617430169810305, 5.000000000000000000 ) ) ;
#55296=VERTEX_POINT ( 'NONE', #7177 ) ;
#55297=EDGE_LOOP ( 'NONE', ( #134422, #44413, #138427, #20326 ) ) ;
#55298=LINE ( 'NONE', #99469, #104398 ) ;
#55299=EDGE_CURVE ( 'NONE', #79224, #117585, #30402, .T. ) ;
#55300=ORIENTED_EDGE ( 'NONE', *, *, #103777, .T. ) ;
#55301=ORIENTED_EDGE ( 'NONE', *, *, #120026, .F. ) ;
#55302=DIRECTION ( 'NONE',  ( -1.000000000000000000, 5.303853817486469551E-15, 0.000000000000000000 ) ) ;
#55303=CARTESIAN_POINT ( 'NONE',  ( 32.28769006033950006, -21.73547319004780931, 4.999917730833664642 ) ) ;
#55304=ORIENTED_EDGE ( 'NONE', *, *, #97632, .F. ) ;
#55305=DIRECTION ( 'NONE',  ( 0.7071067811865487940, -0.7071067811865463515, 0.000000000000000000 ) ) ;
#55306=LINE ( 'NONE', #122676, #123117 ) ;
#55307=EDGE_CURVE ( 'NONE', #81467, #83442, #9306, .T. ) ;
#55308=LINE ( 'NONE', #152, #120419 ) ;
#55309=ADVANCED_FACE ( 'NONE', ( #74637 ), #19516, .T. ) ;
#55312=ORIENTED_EDGE ( 'NONE', *, *, #42696, .T. ) ;
#55313=LINE ( 'NONE', #33579, #30300 ) ;
#55314=CARTESIAN_POINT ( 'NONE',  ( -26.20710678118635784, -2.240707523384255939, 5.000000000000000000 ) ) ;
#55315=CARTESIAN_POINT ( 'NONE',  ( -27.18398860626900060, 28.73617430169806042, 5.000000000000000000 ) ) ;
#55318=CARTESIAN_POINT ( 'NONE',  ( -9.005480084712511157, 28.92564299267931816, 4.000000000000000000 ) ) ;
#55319=FACE_OUTER_BOUND ( 'NONE', #29347, .T. ) ;
#55321=DIRECTION ( 'NONE',  ( -0.000000000000000000, 0.3543493200069153248, 0.9351131265310292928 ) ) ;
#55324=ORIENTED_EDGE ( 'NONE', *, *, #9092, .F. ) ;
#55326=DIRECTION ( 'NONE',  ( -0.7071067811865486830, -0.7071067811865464625, -0.000000000000000000 ) ) ;
#55327=CARTESIAN_POINT ( 'NONE',  ( -30.29974487139158867, -27.71228299555227537, 4.000000000000000000 ) ) ;
#55328=ORIENTED_EDGE ( 'NONE', *, *, #17761, .F. ) ;
#55329=DIRECTION ( 'NONE',  ( -0.7071067811865487940, 0.7071067811865463515, 0.000000000000000000 ) ) ;
#55330=LINE ( 'NONE', #121280, #90934 ) ;
#55331=VECTOR ( 'NONE', #53669, 1000.000000000000227 ) ;
#55335=PLANE ( 'NONE',  #80327 ) ;
#55336=VERTEX_POINT ( 'NONE', #81605 ) ;
#55337=ORIENTED_EDGE ( 'NONE', *, *, #52906, .F. ) ;
#55338=DIRECTION ( 'NONE',  ( -0.6830127018922180770, -0.6830127018922204085, -0.2588190451025213501 ) ) ;
#55340=VECTOR ( 'NONE', #17104, 1000.000000000000000 ) ;
#55341=VECTOR ( 'NONE', #132045, 1000.000000000000000 ) ;
#55344=VECTOR ( 'NONE', #143437, 1000.000000000000000 ) ;
#55345=DIRECTION ( 'NONE',  ( -0.7071067811865486830, -0.7071067811865464625, -0.000000000000000000 ) ) ;
#55346=EDGE_LOOP ( 'NONE', ( #94450, #6313, #111724, #60615 ) ) ;
#55347=PLANE ( 'NONE',  #78967 ) ;
#55349=ORIENTED_EDGE ( 'NONE', *, *, #77740, .F. ) ;
#55351=PLANE ( 'NONE',  #99404 ) ;
#55353=DIRECTION ( 'NONE',  ( -0.7071067811865487940, 0.7071067811865463515, 0.000000000000000000 ) ) ;
#55355=AXIS2_PLACEMENT_3D ( 'NONE', #128389, #48682, #137118 ) ;
#55356=ADVANCED_FACE ( 'NONE', ( #26489 ), #134556, .F. ) ;
#55357=ORIENTED_EDGE ( 'NONE', *, *, #80448, .F. ) ;
#55358=CARTESIAN_POINT ( 'NONE',  ( 36.48921356237310221, -27.52281430457080802, 5.000000000000000000 ) ) ;
#55360=CARTESIAN_POINT ( 'NONE',  ( 22.82816939922337340, -17.24070752338410273, 4.000000000000000000 ) ) ;
#55361=EDGE_CURVE ( 'NONE', #76949, #54350, #104008, .T. ) ;
#55362=DIRECTION ( 'NONE',  ( 0.7071067811865486830, -0.7071067811865464625, -0.000000000000000000 ) ) ;
#55364=VERTEX_POINT ( 'NONE', #13434 ) ;
#55365=EDGE_LOOP ( 'NONE', ( #101900, #64454, #44953, #129974 ) ) ;
#55366=VECTOR ( 'NONE', #130534, 1000.000000000000000 ) ;
#55367=DIRECTION ( 'NONE',  ( -0.6830127018922180770, -0.6830127018922204085, -0.2588190451025213501 ) ) ;
#55368=ORIENTED_EDGE ( 'NONE', *, *, #84415, .F. ) ;
#55369=ADVANCED_FACE ( 'NONE', ( #69292 ), #125815, .F. ) ;
#55370=CARTESIAN_POINT ( 'NONE',  ( -14.99451991528749595, 28.92564299267948513, 4.000000000000000000 ) ) ;
#55371=VERTEX_POINT ( 'NONE', #114883 ) ;
#55372=CARTESIAN_POINT ( 'NONE',  ( 32.67183060077625356, 2.259292476615704981, 4.000000000000000000 ) ) ;
#55373=PLANE ( 'NONE',  #112767 ) ;
#55374=DIRECTION ( 'NONE',  ( -0.000000000000000000, -0.000000000000000000, 1.000000000000000000 ) ) ;
#55376=CARTESIAN_POINT ( 'NONE',  ( 5.187538124160490760, -22.22500000000000142, 4.000000000000000000 ) ) ;
#55378=EDGE_CURVE ( 'NONE', #37141, #132971, #48235, .T. ) ;
#55379=FACE_BOUND ( 'NONE', #52855, .T. ) ;
#55380=DIRECTION ( 'NONE',  ( -0.000000000000000000, -0.3543493200069152693, 0.9351131265310292928 ) ) ;
#55381=PLANE ( 'NONE',  #125474 ) ;
#55382=DIRECTION ( 'NONE',  ( 0.7071067811865487940, 0.7071067811865463515, 0.000000000000000000 ) ) ;
#55383=LINE ( 'NONE', #119871, #29645 ) ;
#55384=ORIENTED_EDGE ( 'NONE', *, *, #67100, .F. ) ;
#55385=VECTOR ( 'NONE', #82412, 1000.000000000000000 ) ;
#55386=VECTOR ( 'NONE', #78421, 1000.000000000000000 ) ;
#55387=FACE_OUTER_BOUND ( 'NONE', #117717, .T. ) ;
#55389=ORIENTED_EDGE ( 'NONE', *, *, #34243, .T. ) ;
#55391=ORIENTED_EDGE ( 'NONE', *, *, #105019, .F. ) ;
#55392=CARTESIAN_POINT ( 'NONE',  ( 26.99999999999980460, 4.965500833774353140, -4.007596771432718974 ) ) ;
#55393=CARTESIAN_POINT ( 'NONE',  ( -30.18398860626900060, 28.73617430169808173, 5.000000000000000000 ) ) ;
#55394=ORIENTED_EDGE ( 'NONE', *, *, #53319, .T. ) ;
#55395=CARTESIAN_POINT ( 'NONE',  ( -34.92500000000001137, -22.22500000000000142, 4.500000000000000888 ) ) ;
#55396=AXIS2_PLACEMENT_3D ( 'NONE', #89316, #55270, #99448 ) ;
#55397=EDGE_CURVE ( 'NONE', #58222, #94758, #46871, .T. ) ;
#55398=ADVANCED_FACE ( 'NONE', ( #93169 ), #2562, .F. ) ;
#55399=CARTESIAN_POINT ( 'NONE',  ( 34.42499999999998295, -3.022814304570575761, 5.000000000000000000 ) ) ;
#55400=DIRECTION ( 'NONE',  ( 0.6830127018922180770, -0.6830127018922204085, -0.2588190451025213501 ) ) ;
#55401=EDGE_CURVE ( 'NONE', #38121, #74158, #24341, .T. ) ;
#55402=CARTESIAN_POINT ( 'NONE',  ( -18.48921356237309510, -27.52281430457068367, 5.000000000000000000 ) ) ;
#55403=CARTESIAN_POINT ( 'NONE',  ( 5.999999999999952927, -13.06887692260767864, 4.000000000000000000 ) ) ;
#55405=ORIENTED_EDGE ( 'NONE', *, *, #66655, .F. ) ;
#55406=EDGE_LOOP ( 'NONE', ( #89001, #5996, #53038, #16049 ) ) ;
#55407=CARTESIAN_POINT ( 'NONE',  ( 48.18398860626899705, 28.73617430169820608, 5.000000000000000000 ) ) ;
#55408=DIRECTION ( 'NONE',  ( -0.7071067811865486830, -0.7071067811865464625, 0.000000000000000000 ) ) ;
#55409=ORIENTED_EDGE ( 'NONE', *, *, #141367, .F. ) ;
#55410=EDGE_LOOP ( 'NONE', ( #44683, #20464, #34630, #55429 ) ) ;
#55411=EDGE_CURVE ( 'NONE', #49875, #129576, #135279, .T. ) ;
#55413=ORIENTED_EDGE ( 'NONE', *, *, #110907, .F. ) ;
#55414=CARTESIAN_POINT ( 'NONE',  ( -45.48921356237309510, -27.52281430457087197, 5.000000000000000000 ) ) ;
#55415=DIRECTION ( 'NONE',  ( -0.6830127018922181881, 0.6830127018922202975, -0.2588190451025214056 ) ) ;
#55417=DIRECTION ( 'NONE',  ( 0.3543493200069163240, 0.000000000000000000, 0.9351131265310288487 ) ) ;
#55418=ORIENTED_EDGE ( 'NONE', *, *, #120799, .T. ) ;
#55419=DIRECTION ( 'NONE',  ( 0.6830127018922180770, -0.6830127018922204085, -0.2588190451025213501 ) ) ;
#55420=ORIENTED_EDGE ( 'NONE', *, *, #114977, .T. ) ;
#55421=CARTESIAN_POINT ( 'NONE',  ( -2.999999999999980016, 7.552185695429095347, 5.000000000000000000 ) ) ;
#55422=LINE ( 'NONE', #134415, #56846 ) ;
#55423=CARTESIAN_POINT ( 'NONE',  ( 0.000000000000000000, 0.000000000000000000, 5.000000000000000000 ) ) ;
#55424=VERTEX_POINT ( 'NONE', #103309 ) ;
#55425=ORIENTED_EDGE ( 'NONE', *, *, #125707, .F. ) ;
#55426=CARTESIAN_POINT ( 'NONE',  ( 18.79289321881332597, 12.75929247661559174, 5.000000000000000000 ) ) ;
#55427=CARTESIAN_POINT ( 'NONE',  ( -34.92500000000001137, -7.298069433178910437, 4.500000000000000888 ) ) ;
#55428=CARTESIAN_POINT ( 'NONE',  ( -0.005480084712502889671, 28.92564299267938210, 4.000000000000000000 ) ) ;
#55429=ORIENTED_EDGE ( 'NONE', *, *, #82284, .T. ) ;
#55433=CARTESIAN_POINT ( 'NONE',  ( -29.99999999999979750, -22.06887692260758271, 4.000000000000000000 ) ) ;
#55434=DIRECTION ( 'NONE',  ( 0.6830127018922181881, 0.6830127018922202975, -0.2588190451025214056 ) ) ;
#55435=VECTOR ( 'NONE', #95811, 1000.000000000000000 ) ;
#55436=VECTOR ( 'NONE', #102288, 1000.000000000000000 ) ;
#55440=FACE_OUTER_BOUND ( 'NONE', #63541, .T. ) ;
#55441=VECTOR ( 'NONE', #33987, 1000.000000000000000 ) ;
#55442=DIRECTION ( 'NONE',  ( 0.7071067811865487940, -0.7071067811865463515, 0.000000000000000000 ) ) ;
#55443=LINE ( 'NONE', #111972, #136294 ) ;
#55444=ORIENTED_EDGE ( 'NONE', *, *, #18560, .T. ) ;
#55445=CARTESIAN_POINT ( 'NONE',  ( 25.17183060077629975, 6.759292476615649470, 4.000000000000000000 ) ) ;
#55446=ORIENTED_EDGE ( 'NONE', *, *, #58814, .T. ) ;
#55447=VECTOR ( 'NONE', #80444, 1000.000000000000000 ) ;
#55448=CARTESIAN_POINT ( 'NONE',  ( -9.299744871391588674, -27.71228299555212971, 4.000000000000000000 ) ) ;
#55449=DIRECTION ( 'NONE',  ( 0.7071067811865487940, 0.7071067811865463515, 0.000000000000000000 ) ) ;
#55450=EDGE_CURVE ( 'NONE', #35713, #7390, #38095, .T. ) ;
#55451=ORIENTED_EDGE ( 'NONE', *, *, #26724, .F. ) ;
#55452=CARTESIAN_POINT ( 'NONE',  ( 14.20710678118644310, 15.75929247661555443, 5.000000000000000000 ) ) ;
#55453=DIRECTION ( 'NONE',  ( -0.7071067811865487940, 0.7071067811865463515, 0.000000000000000000 ) ) ;
#55454=CARTESIAN_POINT ( 'NONE',  ( -48.18398860626899705, 28.73617430169820608, 5.000000000000000000 ) ) ;
#55456=EDGE_LOOP ( 'NONE', ( #113702, #73259, #69515, #418 ) ) ;
#55458=LINE ( 'NONE', #78633, #16371 ) ;
#55459=EDGE_CURVE ( 'NONE', #7608, #64278, #3960, .T. ) ;
#55460=CARTESIAN_POINT ( 'NONE',  ( -20.99999999999985079, -13.39766691384885000, -10.96608748226461039 ) ) ;
#55462=AXIS2_PLACEMENT_3D ( 'NONE', #65637, #22062, #9006 ) ;
#55463=DIRECTION ( 'NONE',  ( 0.7071067811865486830, -0.7071067811865464625, -0.000000000000000000 ) ) ;
#55464=CARTESIAN_POINT ( 'NONE',  ( 3.489213562373097322, -27.52281430457057709, 5.000000000000000000 ) ) ;
#55465=EDGE_CURVE ( 'NONE', #115745, #65695, #80184, .T. ) ;
#55468=AXIS2_PLACEMENT_3D ( 'NONE', #111843, #58217, #90813 ) ;
#55471=PLANE ( 'NONE',  #111272 ) ;
#55472=ORIENTED_EDGE ( 'NONE', *, *, #26830, .F. ) ;
#55473=DIRECTION ( 'NONE',  ( 0.7071067811865487940, 0.7071067811865463515, 0.000000000000000000 ) ) ;
#55474=ORIENTED_EDGE ( 'NONE', *, *, #25210, .F. ) ;
#55475=FACE_OUTER_BOUND ( 'NONE', #75291, .T. ) ;
#55476=CARTESIAN_POINT ( 'NONE',  ( 3.489213562373097322, -27.52281430457057709, 5.000000000000000000 ) ) ;
#55478=AXIS2_PLACEMENT_3D ( 'NONE', #80629, #84218, #105214 ) ;
#55479=VECTOR ( 'NONE', #66350, 1000.000000000000000 ) ;
#55480=LINE ( 'NONE', #133055, #46182 ) ;
#55483=EDGE_CURVE ( 'NONE', #70680, #136170, #122949, .T. ) ;
#55484=CARTESIAN_POINT ( 'NONE',  ( 7.499999999999946709, 22.01701374228155572, 2.453858888625611634 ) ) ;
#55486=ORIENTED_EDGE ( 'NONE', *, *, #52529, .F. ) ;
#55487=AXIS2_PLACEMENT_3D ( 'NONE', #107531, #48893, #18348 ) ;
#55488=VERTEX_POINT ( 'NONE', #135958 ) ;
#55489=LINE ( 'NONE', #99671, #101915 ) ;
#55491=AXIS2_PLACEMENT_3D ( 'NONE', #24823, #124139, #123463 ) ;
#55492=LINE ( 'NONE', #43187, #38158 ) ;
#55493=ADVANCED_FACE ( 'NONE', ( #80884 ), #67898, .F. ) ;
#55494=DIRECTION ( 'NONE',  ( -0.7071067811865486830, -0.7071067811865464625, 0.000000000000000000 ) ) ;
#55496=CARTESIAN_POINT ( 'NONE',  ( -30.18398860626900060, 28.73617430169808173, 5.000000000000000000 ) ) ;
#55497=LINE ( 'NONE', #45355, #43766 ) ;
#55498=EDGE_LOOP ( 'NONE', ( #2068, #17184, #87312, #26398 ) ) ;
#55500=DIRECTION ( 'NONE',  ( -0.000000000000000000, 0.000000000000000000, 1.000000000000000000 ) ) ;
#55501=LINE ( 'NONE', #47515, #104069 ) ;
#55503=ADVANCED_FACE ( 'NONE', ( #79495 ), #112776, .F. ) ;
#55504=VECTOR ( 'NONE', #80442, 1000.000000000000000 ) ;
#55505=EDGE_LOOP ( 'NONE', ( #8999, #135421, #85823, #32093 ) ) ;
#55506=PLANE ( 'NONE',  #12039 ) ;
#55507=ORIENTED_EDGE ( 'NONE', *, *, #89308, .T. ) ;
#55510=DIRECTION ( 'NONE',  ( 0.7071067811865487940, 0.7071067811865463515, 0.000000000000000000 ) ) ;
#55511=EDGE_CURVE ( 'NONE', #78692, #12567, #127961, .T. ) ;
#55512=VERTEX_POINT ( 'NONE', #93876 ) ;
#55513=DIRECTION ( 'NONE',  ( -0.000000000000000000, -0.3543493200069152693, 0.9351131265310292928 ) ) ;
#55514=LINE ( 'NONE', #95603, #63753 ) ;
#55515=CARTESIAN_POINT ( 'NONE',  ( -34.49999999999975131, 9.054329344830845727, 4.994342998332165884 ) ) ;
#55517=DIRECTION ( 'NONE',  ( 0.3543493200069162685, -0.000000000000000000, -0.9351131265310288487 ) ) ;
#55518=LINE ( 'NONE', #76567, #130981 ) ;
#55519=EDGE_LOOP ( 'NONE', ( #71493, #66023, #80393 ) ) ;
#55520=DIRECTION ( 'NONE',  ( 0.7071067811865487940, 0.7071067811865463515, 0.000000000000000000 ) ) ;
#55521=CARTESIAN_POINT ( 'NONE',  ( 0.000000000000000000, 0.000000000000000000, 5.000000000000000000 ) ) ;
#55522=DIRECTION ( 'NONE',  ( -0.7071067811865486830, -0.7071067811865464625, -0.000000000000000000 ) ) ;
#55523=EDGE_LOOP ( 'NONE', ( #127743, #32711, #62550, #60282, #142153 ) ) ;
#55524=ADVANCED_FACE ( 'NONE', ( #63437 ), #18423, .F. ) ;
#55525=ORIENTED_EDGE ( 'NONE', *, *, #53984, .F. ) ;
#55527=VERTEX_POINT ( 'NONE', #116347 ) ;
#55528=DIRECTION ( 'NONE',  ( -0.000000000000000000, -0.3543493200069152693, 0.9351131265310292928 ) ) ;
#55529=DIRECTION ( 'NONE',  ( -0.000000000000000000, -0.3543493200069152693, 0.9351131265310292928 ) ) ;
#55530=DIRECTION ( 'NONE',  ( -1.000000000000000000, 0.000000000000000000, -0.000000000000000000 ) ) ;
#55531=ADVANCED_FACE ( 'NONE', ( #6112 ), #40250, .F. ) ;
#55532=PLANE ( 'NONE',  #38796 ) ;
#55534=VERTEX_POINT ( 'NONE', #38795 ) ;
#55535=EDGE_LOOP ( 'NONE', ( #112497, #93498, #79456, #75730 ) ) ;
#55536=CARTESIAN_POINT ( 'NONE',  ( -24.48921356237309510, -27.52281430457072631, 5.000000000000000000 ) ) ;
#55537=ORIENTED_EDGE ( 'NONE', *, *, #101078, .F. ) ;
#55539=FACE_OUTER_BOUND ( 'NONE', #54237, .T. ) ;
#55541=PLANE ( 'NONE',  #51572 ) ;
#55542=AXIS2_PLACEMENT_3D ( 'NONE', #55237, #68290, #33507 ) ;
#55546=EDGE_LOOP ( 'NONE', ( #142667, #113411, #54571, #77661 ) ) ;
#55547=AXIS2_PLACEMENT_3D ( 'NONE', #135126, #91587, #3807 ) ;
#55549=FACE_BOUND ( 'NONE', #85176, .T. ) ;
#55550=CARTESIAN_POINT ( 'NONE',  ( 30.06011071044001426, -9.740707523384180888, 10.89222023123373795 ) ) ;
#55553=VECTOR ( 'NONE', #30144, 1000.000000000000227 ) ;
#55554=CARTESIAN_POINT ( 'NONE',  ( -27.48921356237309155, -27.52281430457074762, 5.000000000000000000 ) ) ;
#55558=VECTOR ( 'NONE', #137285, 1000.000000000000000 ) ;
#55559=ORIENTED_EDGE ( 'NONE', *, *, #17999, .F. ) ;
#55561=ORIENTED_EDGE ( 'NONE', *, *, #118681, .F. ) ;
#55562=ORIENTED_EDGE ( 'NONE', *, *, #142023, .F. ) ;
#55563=AXIS2_PLACEMENT_3D ( 'NONE', #8858, #79232, #90795 ) ;
#55564=VECTOR ( 'NONE', #69410, 1000.000000000000000 ) ;
#55566=FACE_OUTER_BOUND ( 'NONE', #58126, .T. ) ;
#55568=CARTESIAN_POINT ( 'NONE',  ( -45.29974487139158867, -27.71228299555237840, 4.000000000000000000 ) ) ;
#55569=ORIENTED_EDGE ( 'NONE', *, *, #12886, .F. ) ;
#55570=DIRECTION ( 'NONE',  ( 0.6830127018922180770, -0.6830127018922204085, -0.2588190451025213501 ) ) ;
#55571=DIRECTION ( 'NONE',  ( 0.7071067811865487940, -0.7071067811865463515, 0.000000000000000000 ) ) ;
#55572=EDGE_CURVE ( 'NONE', #138636, #19628, #62704, .T. ) ;
#55574=CARTESIAN_POINT ( 'NONE',  ( 30.18398860626900060, 28.73617430169808173, 5.000000000000000000 ) ) ;
#55576=PLANE ( 'NONE',  #11405 ) ;
#55578=VERTEX_POINT ( 'NONE', #52511 ) ;
#55579=VECTOR ( 'NONE', #23177, 1000.000000000000227 ) ;
#55581=CARTESIAN_POINT ( 'NONE',  ( -2.999999999999975131, -21.84840872380824450, 2.849755605029599348 ) ) ;
#55582=VERTEX_POINT ( 'NONE', #72178 ) ;
#55583=ADVANCED_FACE ( 'NONE', ( #51827 ), #129353, .F. ) ;
#55584=ORIENTED_EDGE ( 'NONE', *, *, #110633, .F. ) ;
#55585=VECTOR ( 'NONE', #37626, 1000.000000000000227 ) ;
#55586=EDGE_CURVE ( 'NONE', #81677, #35253, #106886, .T. ) ;
#55587=VERTEX_POINT ( 'NONE', #140943 ) ;
#55588=EDGE_CURVE ( 'NONE', #6599, #20040, #61998, .T. ) ;
#55591=ORIENTED_EDGE ( 'NONE', *, *, #30383, .F. ) ;
#55592=CARTESIAN_POINT ( 'NONE',  ( -15.48921356237309510, -27.52281430457066236, 5.000000000000000000 ) ) ;
#55596=CARTESIAN_POINT ( 'NONE',  ( -34.47516574401890210, 19.49051761211541844, 4.998110765256836174 ) ) ;
#55598=LINE ( 'NONE', #99787, #125169 ) ;
#55599=AXIS2_PLACEMENT_3D ( 'NONE', #136576, #80105, #72092 ) ;
#55600=LINE ( 'NONE', #9170, #19217 ) ;
#55601=EDGE_CURVE ( 'NONE', #121901, #84862, #117740, .T. ) ;
#55602=FACE_OUTER_BOUND ( 'NONE', #117868, .T. ) ;
#55603=ORIENTED_EDGE ( 'NONE', *, *, #6028, .T. ) ;
#55604=PLANE ( 'NONE',  #52721 ) ;
#55605=CARTESIAN_POINT ( 'NONE',  ( 48.48921356237309510, -27.52281430457089328, 5.000000000000000000 ) ) ;
#55607=ORIENTED_EDGE ( 'NONE', *, *, #11354, .T. ) ;
#55608=ORIENTED_EDGE ( 'NONE', *, *, #111181, .T. ) ;
#55610=VECTOR ( 'NONE', #1685, 1000.000000000000227 ) ;
#55611=CARTESIAN_POINT ( 'NONE',  ( -17.99451991528748351, 28.92564299267950645, 4.000000000000000000 ) ) ;
#55612=CARTESIAN_POINT ( 'NONE',  ( 14.51078643762690490, -27.52281430457045275, 5.000000000000000000 ) ) ;
#55613=ORIENTED_EDGE ( 'NONE', *, *, #17034, .F. ) ;
#55614=LINE ( 'NONE', #132491, #46537 ) ;
#55615=ORIENTED_EDGE ( 'NONE', *, *, #59166, .T. ) ;
#55616=VECTOR ( 'NONE', #100579, 1000.000000000000000 ) ;
#55618=EDGE_CURVE ( 'NONE', #26139, #83438, #5418, .T. ) ;
#55619=LINE ( 'NONE', #54909, #52911 ) ;
#55620=DIRECTION ( 'NONE',  ( -0.7071067811865487940, 0.7071067811865463515, 0.000000000000000000 ) ) ;
#55621=VERTEX_POINT ( 'NONE', #74286 ) ;
#55622=ADVANCED_FACE ( 'NONE', ( #7565 ), #30039, .F. ) ;
#55624=ORIENTED_EDGE ( 'NONE', *, *, #106167, .F. ) ;
#55626=PLANE ( 'NONE',  #4650 ) ;
#55627=LINE ( 'NONE', #133893, #126026 ) ;
#55628=CARTESIAN_POINT ( 'NONE',  ( -57.18398860626899705, 28.73617430169827358, 5.000000000000000000 ) ) ;
#55629=EDGE_CURVE ( 'NONE', #30840, #52778, #138105, .T. ) ;
#55630=ADVANCED_FACE ( 'NONE', ( #29328 ), #73570, .T. ) ;
#55632=CARTESIAN_POINT ( 'NONE',  ( 34.82816939922328459, -5.240707523384228850, 4.000000000000000000 ) ) ;
#55633=LINE ( 'NONE', #57793, #109677 ) ;
#55634=CARTESIAN_POINT ( 'NONE',  ( 31.49999999999977973, -2.568876922607791879, 4.000000000000000000 ) ) ;
#55635=DIRECTION ( 'NONE',  ( -0.000000000000000000, -0.000000000000000000, 1.000000000000000000 ) ) ;
#55636=ORIENTED_EDGE ( 'NONE', *, *, #43042, .F. ) ;
#55637=CARTESIAN_POINT ( 'NONE',  ( 42.18398860626899705, 28.73617430169816700, 5.000000000000000000 ) ) ;
#55638=ORIENTED_EDGE ( 'NONE', *, *, #132761, .F. ) ;
#55640=AXIS2_PLACEMENT_3D ( 'NONE', #109468, #110159, #67419 ) ;
#55641=CARTESIAN_POINT ( 'NONE',  ( 8.816011393731004731, 28.73617430169781173, 5.000000000000000000 ) ) ;
#55643=VECTOR ( 'NONE', #49181, 1000.000000000000000 ) ;
#55644=PLANE ( 'NONE',  #46077 ) ;
#55646=EDGE_LOOP ( 'NONE', ( #41986, #110789, #109872, #31438 ) ) ;
#55647=ADVANCED_FACE ( 'NONE', ( #60581 ), #49698, .F. ) ;
#55648=EDGE_CURVE ( 'NONE', #141315, #132971, #109022, .T. ) ;
#55649=DIRECTION ( 'NONE',  ( -0.000000000000000000, 0.000000000000000000, 1.000000000000000000 ) ) ;
#55650=DIRECTION ( 'NONE',  ( 0.7071067811865487940, 0.7071067811865463515, 0.000000000000000000 ) ) ;
#55651=ORIENTED_EDGE ( 'NONE', *, *, #46310, .F. ) ;
#55652=DIRECTION ( 'NONE',  ( 0.7071067811865486830, -0.7071067811865464625, -0.000000000000000000 ) ) ;
#55653=VERTEX_POINT ( 'NONE', #131517 ) ;
#55654=CARTESIAN_POINT ( 'NONE',  ( 12.32816939922344623, -21.74070752338406365, 4.000000000000000000 ) ) ;
#55655=VECTOR ( 'NONE', #128939, 1000.000000000000000 ) ;
#55656=ORIENTED_EDGE ( 'NONE', *, *, #108416, .T. ) ;
#55657=DIRECTION ( 'NONE',  ( -0.7071067811865486830, -0.7071067811865464625, -0.000000000000000000 ) ) ;
#55659=EDGE_CURVE ( 'NONE', #106208, #55894, #122036, .T. ) ;
#55660=CARTESIAN_POINT ( 'NONE',  ( 26.99451991528749417, 28.92564299267956685, 4.000000000000000000 ) ) ;
#55661=DIRECTION ( 'NONE',  ( 0.7071067811865487940, 0.7071067811865463515, 0.000000000000000000 ) ) ;
#55662=DIRECTION ( 'NONE',  ( 0.000000000000000000, 1.000000000000000000, 0.000000000000000000 ) ) ;
#55666=VECTOR ( 'NONE', #16549, 1000.000000000000000 ) ;
#55667=EDGE_CURVE ( 'NONE', #39610, #14791, #87298, .T. ) ;
#55668=DIRECTION ( 'NONE',  ( -0.3543493200069162685, -0.000000000000000000, -0.9351131265310288487 ) ) ;
#55669=CARTESIAN_POINT ( 'NONE',  ( 5.510786437626906675, -27.52281430457051314, 5.000000000000000000 ) ) ;
#55670=EDGE_LOOP ( 'NONE', ( #73152, #23853, #80217, #84097 ) ) ;
#55671=ORIENTED_EDGE ( 'NONE', *, *, #79862, .T. ) ;
#55672=VECTOR ( 'NONE', #108234, 1000.000000000000000 ) ;
#55673=CARTESIAN_POINT ( 'NONE',  ( -16.49999999999988631, -8.568876922607724822, 4.000000000000000000 ) ) ;
#55675=VECTOR ( 'NONE', #105295, 1000.000000000000227 ) ;
#55677=VECTOR ( 'NONE', #74203, 1000.000000000000000 ) ;
#55678=DIRECTION ( 'NONE',  ( 0.3543493200069162685, -0.000000000000000000, -0.9351131265310288487 ) ) ;
#55679=DIRECTION ( 'NONE',  ( 0.7071067811865486830, -0.7071067811865464625, -0.000000000000000000 ) ) ;
#55681=LINE ( 'NONE', #99879, #60947 ) ;
#55683=ORIENTED_EDGE ( 'NONE', *, *, #16193, .F. ) ;
#55684=VECTOR ( 'NONE', #91648, 1000.000000000000000 ) ;
#55685=CARTESIAN_POINT ( 'NONE',  ( -21.70710678118638626, -12.74070752338415424, 5.000000000000000000 ) ) ;
#55687=DIRECTION ( 'NONE',  ( -0.7071067811865487940, 0.7071067811865463515, 0.000000000000000000 ) ) ;
#55690=DIRECTION ( 'NONE',  ( 0.7071067811865487940, -0.7071067811865463515, 0.000000000000000000 ) ) ;
#55691=EDGE_CURVE ( 'NONE', #106470, #119037, #43792, .T. ) ;
#55692=VERTEX_POINT ( 'NONE', #76432 ) ;
#55693=FACE_OUTER_BOUND ( 'NONE', #41242, .T. ) ;
#55694=ADVANCED_FACE ( 'NONE', ( #19876 ), #120602, .F. ) ;
#55695=CARTESIAN_POINT ( 'NONE',  ( 21.18398860626899349, 28.73617430169802134, 5.000000000000000000 ) ) ;
#55696=DIRECTION ( 'NONE',  ( -8.817971600062198362E-18, -0.3543493200069152693, 0.9351131265310292928 ) ) ;
#55697=CARTESIAN_POINT ( 'NONE',  ( 11.70025512860841133, -27.71228299555198049, 4.000000000000000000 ) ) ;
#55698=DIRECTION ( 'NONE',  ( -0.6830127018922181881, 0.6830127018922202975, -0.2588190451025214056 ) ) ;
#55699=ORIENTED_EDGE ( 'NONE', *, *, #132401, .F. ) ;
#55700=ADVANCED_FACE ( 'NONE', ( #10424 ), #98174, .F. ) ;
#55701=ORIENTED_EDGE ( 'NONE', *, *, #73165, .T. ) ;
#55702=ORIENTED_EDGE ( 'NONE', *, *, #84282, .T. ) ;
#55704=VECTOR ( 'NONE', #119102, 1000.000000000000227 ) ;
#55705=VERTEX_POINT ( 'NONE', #243 ) ;
#55706=CARTESIAN_POINT ( 'NONE',  ( 1.171830600776462061, -8.240707523384200428, 4.000000000000000000 ) ) ;
#55707=CARTESIAN_POINT ( 'NONE',  ( 3.005480084712505828, 28.92564299267936079, 4.000000000000000000 ) ) ;
#55708=CARTESIAN_POINT ( 'NONE',  ( 0.000000000000000000, 0.000000000000000000, 5.000000000000000000 ) ) ;
#55709=PLANE ( 'NONE',  #121840 ) ;
#55710=EDGE_LOOP ( 'NONE', ( #35453, #35719, #58700, #48298 ) ) ;
#55711=CARTESIAN_POINT ( 'NONE',  ( -16.82816939922341248, 15.75929247661555443, 4.000000000000000000 ) ) ;
#55715=CARTESIAN_POINT ( 'NONE',  ( 34.92499999999998295, 22.22500000000000142, 4.500000000000000888 ) ) ;
#55717=VECTOR ( 'NONE', #13832, 1000.000000000000000 ) ;
#55718=ORIENTED_EDGE ( 'NONE', *, *, #69315, .F. ) ;
#55719=VERTEX_POINT ( 'NONE', #88005 ) ;
#55721=PLANE ( 'NONE',  #113980 ) ;
#55724=CARTESIAN_POINT ( 'NONE',  ( -2.207106781186525701, 0.7592924766157052030, 5.000000000000000000 ) ) ;
#55725=VECTOR ( 'NONE', #111070, 1000.000000000000000 ) ;
#55726=VECTOR ( 'NONE', #32628, 1000.000000000000000 ) ;
#55728=DIRECTION ( 'NONE',  ( -0.3543493200069162685, -0.000000000000000000, -0.9351131265310288487 ) ) ;
#55730=ORIENTED_EDGE ( 'NONE', *, *, #120508, .F. ) ;
#55731=ORIENTED_EDGE ( 'NONE', *, *, #39218, .T. ) ;
#55732=FACE_OUTER_BOUND ( 'NONE', #15653, .T. ) ;
#55733=ORIENTED_EDGE ( 'NONE', *, *, #137999, .T. ) ;
#55734=EDGE_LOOP ( 'NONE', ( #138827, #103108, #109318, #66045 ) ) ;
#55735=AXIS2_PLACEMENT_3D ( 'NONE', #133522, #69716, #113167 ) ;
#55737=AXIS2_PLACEMENT_3D ( 'NONE', #10392, #130795, #74987 ) ;
#55739=ORIENTED_EDGE ( 'NONE', *, *, #103877, .F. ) ;
#55741=CARTESIAN_POINT ( 'NONE',  ( -3.707013264293017141, -21.74070752338405299, 4.999753212805222446 ) ) ;
#55742=FACE_OUTER_BOUND ( 'NONE', #90857, .T. ) ;
#55743=CARTESIAN_POINT ( 'NONE',  ( 18.00548008471250583, 28.92564299267925776, 4.000000000000000000 ) ) ;
#55745=AXIS2_PLACEMENT_3D ( 'NONE', #74549, #115852, #139084 ) ;
#55746=VECTOR ( 'NONE', #60825, 1000.000000000000000 ) ;
#55747=VECTOR ( 'NONE', #127733, 1000.000000000000000 ) ;
#55749=ORIENTED_EDGE ( 'NONE', *, *, #116715, .T. ) ;
#55750=AXIS2_PLACEMENT_3D ( 'NONE', #78595, #100352, #56167 ) ;
#55752=ORIENTED_EDGE ( 'NONE', *, *, #14030, .T. ) ;
#55754=CARTESIAN_POINT ( 'NONE',  ( 28.60343192894626441, -14.24070752338413293, 19.24067776001732355 ) ) ;
#55757=ORIENTED_EDGE ( 'NONE', *, *, #103576, .T. ) ;
#55758=CARTESIAN_POINT ( 'NONE',  ( 30.18398860626900060, 28.73617430169808173, 5.000000000000000000 ) ) ;
#55759=EDGE_CURVE ( 'NONE', #53631, #131121, #130826, .T. ) ;
#55763=ORIENTED_EDGE ( 'NONE', *, *, #96244, .T. ) ;
#55764=DIRECTION ( 'NONE',  ( 0.7071067811865486830, -0.7071067811865464625, -0.000000000000000000 ) ) ;
#55765=CARTESIAN_POINT ( 'NONE',  ( 42.48921356237308800, -27.52281430457085065, 5.000000000000000000 ) ) ;
#55767=DIRECTION ( 'NONE',  ( -0.6830127018922181881, 0.6830127018922202975, -0.2588190451025214056 ) ) ;
#55768=EDGE_CURVE ( 'NONE', #103662, #138649, #121335, .T. ) ;
#55770=CARTESIAN_POINT ( 'NONE',  ( 0.000000000000000000, 0.000000000000000000, 5.000000000000000000 ) ) ;
#55771=FACE_OUTER_BOUND ( 'NONE', #7370, .T. ) ;
#55772=AXIS2_PLACEMENT_3D ( 'NONE', #10659, #44043, #142637 ) ;
#55773=FACE_OUTER_BOUND ( 'NONE', #10441, .T. ) ;
#55774=ADVANCED_FACE ( 'NONE', ( #119883 ), #22021, .F. ) ;
#55775=VECTOR ( 'NONE', #48396, 1000.000000000000227 ) ;
#55776=CARTESIAN_POINT ( 'NONE',  ( -51.48921356237309510, -27.52281430457091460, 5.000000000000000000 ) ) ;
#55777=VERTEX_POINT ( 'NONE', #66269 ) ;
#55778=DIRECTION ( 'NONE',  ( 0.6830127018922181881, 0.6830127018922202975, -0.2588190451025214056 ) ) ;
#55779=DIRECTION ( 'NONE',  ( -0.6830127018922180770, -0.6830127018922204085, -0.2588190451025213501 ) ) ;
#55780=ORIENTED_EDGE ( 'NONE', *, *, #77263, .T. ) ;
#55781=VECTOR ( 'NONE', #889, 1000.000000000000227 ) ;
#55782=ORIENTED_EDGE ( 'NONE', *, *, #88853, .T. ) ;
#55783=EDGE_LOOP ( 'NONE', ( #140107, #67204, #124750, #79497, #61245, #30876 ) ) ;
#55785=EDGE_CURVE ( 'NONE', #19566, #108338, #11117, .T. ) ;
#55786=VERTEX_POINT ( 'NONE', #44542 ) ;
#55788=DIRECTION ( 'NONE',  ( 0.7071067811865487940, 0.7071067811865463515, 0.000000000000000000 ) ) ;
#55789=CARTESIAN_POINT ( 'NONE',  ( 34.92499999999998295, 22.22500000000000142, 4.000000000000000000 ) ) ;
#55790=PLANE ( 'NONE',  #34074 ) ;
#55791=VECTOR ( 'NONE', #71332, 1000.000000000000000 ) ;
#55792=CARTESIAN_POINT ( 'NONE',  ( -11.21342912940201764, -22.22500000000000142, -3.985200587934857541 ) ) ;
#55793=CARTESIAN_POINT ( 'NONE',  ( -4.265066702820487166, 12.75929247661558996, 18.34774599283957386 ) ) ;
#55795=DIRECTION ( 'NONE',  ( 0.7071067811865487940, 0.7071067811865463515, -0.000000000000000000 ) ) ;
#55796=EDGE_CURVE ( 'NONE', #40167, #25993, #85854, .T. ) ;
#55797=ORIENTED_EDGE ( 'NONE', *, *, #118797, .F. ) ;
#55799=VECTOR ( 'NONE', #44442, 1000.000000000000000 ) ;
#55801=VERTEX_POINT ( 'NONE', #130091 ) ;
#55804=LINE ( 'NONE', #110833, #95128 ) ;
#55805=ORIENTED_EDGE ( 'NONE', *, *, #114669, .T. ) ;
#55806=EDGE_CURVE ( 'NONE', #110443, #65489, #132973, .T. ) ;
#55807=ORIENTED_EDGE ( 'NONE', *, *, #98234, .F. ) ;
#55809=VERTEX_POINT ( 'NONE', #64118 ) ;
#55810=CARTESIAN_POINT ( 'NONE',  ( 20.99999999999985079, -5.527737879153171718, -7.983877177622420440 ) ) ;
#55811=CARTESIAN_POINT ( 'NONE',  ( -10.49999999999992184, 4.466399257802213363, 5.000000000000000000 ) ) ;
#55813=CARTESIAN_POINT ( 'NONE',  ( 34.92499999999998295, -21.72500000000000142, 5.000000000000000000 ) ) ;
#55814=VECTOR ( 'NONE', #112327, 999.9999999999998863 ) ;
#55815=LINE ( 'NONE', #100019, #116798 ) ;
#55816=ORIENTED_EDGE ( 'NONE', *, *, #1767, .F. ) ;
#55817=EDGE_CURVE ( 'NONE', #72918, #121606, #119193, .T. ) ;
#55818=EDGE_CURVE ( 'NONE', #52838, #99485, #64837, .T. ) ;
#55820=DIRECTION ( 'NONE',  ( -0.7071067811865486830, -0.7071067811865464625, 0.000000000000000000 ) ) ;
#55821=ORIENTED_EDGE ( 'NONE', *, *, #140099, .F. ) ;
#55823=VECTOR ( 'NONE', #47621, 1000.000000000000000 ) ;
#55825=ADVANCED_FACE ( 'NONE', ( #90885 ), #70581, .F. ) ;
#55827=DIRECTION ( 'NONE',  ( -0.3543493200069162685, -0.000000000000000000, -0.9351131265310288487 ) ) ;
#55828=VERTEX_POINT ( 'NONE', #112613 ) ;
#55829=EDGE_CURVE ( 'NONE', #134528, #33663, #35804, .T. ) ;
#55830=ORIENTED_EDGE ( 'NONE', *, *, #34768, .F. ) ;
#55831=EDGE_CURVE ( 'NONE', #41910, #64188, #114727, .T. ) ;
#55832=CARTESIAN_POINT ( 'NONE',  ( -48.18398860626899705, 28.73617430169820608, 5.000000000000000000 ) ) ;
#55833=DIRECTION ( 'NONE',  ( 0.7071067811865487940, -0.7071067811865463515, 0.000000000000000000 ) ) ;
#55834=VECTOR ( 'NONE', #53722, 1000.000000000000000 ) ;
#55835=ORIENTED_EDGE ( 'NONE', *, *, #67569, .T. ) ;
#55837=PLANE ( 'NONE',  #27696 ) ;
#55838=EDGE_CURVE ( 'NONE', #20875, #1659, #971, .T. ) ;
#55839=LINE ( 'NONE', #696, #99409 ) ;
#55840=DIRECTION ( 'NONE',  ( -0.6830127018922180770, -0.6830127018922204085, -0.2588190451025213501 ) ) ;
#55841=LINE ( 'NONE', #44250, #70010 ) ;
#55842=CARTESIAN_POINT ( 'NONE',  ( 72.48921356237309510, -27.52281430457106026, 5.000000000000000000 ) ) ;
#55845=PLANE ( 'NONE',  #88527 ) ;
#55847=VECTOR ( 'NONE', #37789, 1000.000000000000000 ) ;
#55849=DIRECTION ( 'NONE',  ( -0.6830127018922180770, -0.6830127018922204085, -0.2588190451025213501 ) ) ;
#55850=CARTESIAN_POINT ( 'NONE',  ( -34.49999999999976552, 8.900465351122123892, -2.516491619111432154 ) ) ;
#55851=EDGE_LOOP ( 'NONE', ( #73952, #100512, #53176, #127557 ) ) ;
#55852=VERTEX_POINT ( 'NONE', #123522 ) ;
#55855=VECTOR ( 'NONE', #71239, 1000.000000000000000 ) ;
#55856=EDGE_LOOP ( 'NONE', ( #94381, #65888, #44744, #123662 ) ) ;
#55858=ORIENTED_EDGE ( 'NONE', *, *, #14695, .T. ) ;
#55860=DIRECTION ( 'NONE',  ( 0.7071067811865487940, 0.7071067811865463515, 0.000000000000000000 ) ) ;
#55863=VECTOR ( 'NONE', #139989, 1000.000000000000227 ) ;
#55864=VECTOR ( 'NONE', #109355, 1000.000000000000000 ) ;
#55865=ORIENTED_EDGE ( 'NONE', *, *, #54482, .T. ) ;
#55866=LINE ( 'NONE', #88485, #18476 ) ;
#55867=VECTOR ( 'NONE', #127077, 1000.000000000000000 ) ;
#55868=CARTESIAN_POINT ( 'NONE',  ( 13.10332671766740020, 3.690788593506699300, 4.000000000000000000 ) ) ;
#55869=CARTESIAN_POINT ( 'NONE',  ( -28.49999999999979750, 1.466399257802248446, 5.000000000000000000 ) ) ;
#55870=ORIENTED_EDGE ( 'NONE', *, *, #90630, .T. ) ;
#55871=DIRECTION ( 'NONE',  ( -0.6830127018922181881, 0.6830127018922202975, -0.2588190451025214056 ) ) ;
#55872=FACE_OUTER_BOUND ( 'NONE', #138437, .T. ) ;
#55873=AXIS2_PLACEMENT_3D ( 'NONE', #136612, #94527, #70691 ) ;
#55874=CARTESIAN_POINT ( 'NONE',  ( 34.92499999999998295, 14.71849043720411387, 4.759050581649326261 ) ) ;
#55876=DIRECTION ( 'NONE',  ( 1.000000000000000000, 0.000000000000000000, 0.000000000000000000 ) ) ;
#55879=CARTESIAN_POINT ( 'NONE',  ( -60.18398860626900415, 28.73617430169829490, 5.000000000000000000 ) ) ;
#55880=EDGE_CURVE ( 'NONE', #42960, #39646, #25586, .T. ) ;
#55881=EDGE_CURVE ( 'NONE', #131796, #88687, #26324, .T. ) ;
#55882=ORIENTED_EDGE ( 'NONE', *, *, #25225, .F. ) ;
#55883=ORIENTED_EDGE ( 'NONE', *, *, #119868, .F. ) ;
#55886=AXIS2_PLACEMENT_3D ( 'NONE', #101180, #1821, #35252 ) ;
#55887=CARTESIAN_POINT ( 'NONE',  ( -3.183988606268992161, 28.73617430169789699, 5.000000000000000000 ) ) ;
#55888=CARTESIAN_POINT ( 'NONE',  ( 12.48921356237309155, -27.52281430457064104, 5.000000000000000000 ) ) ;
#55889=EDGE_CURVE ( 'NONE', #91367, #49119, #134380, .T. ) ;
#55890=CARTESIAN_POINT ( 'NONE',  ( 42.48921356237308800, -27.52281430457085065, 5.000000000000000000 ) ) ;
#55891=VECTOR ( 'NONE', #92987, 1000.000000000000227 ) ;
#55892=AXIS2_PLACEMENT_3D ( 'NONE', #4827, #36108, #58616 ) ;
#55894=VERTEX_POINT ( 'NONE', #24181 ) ;
#55895=VECTOR ( 'NONE', #56511, 1000.000000000000000 ) ;
#55897=DIRECTION ( 'NONE',  ( -0.7071067811865486830, -0.7071067811865464625, -0.000000000000000000 ) ) ;
#55898=LINE ( 'NONE', #100096, #24604 ) ;
#55899=ORIENTED_EDGE ( 'NONE', *, *, #99142, .T. ) ;
#55900=ORIENTED_EDGE ( 'NONE', *, *, #23027, .F. ) ;
#55902=ORIENTED_EDGE ( 'NONE', *, *, #36949, .T. ) ;
#55903=VECTOR ( 'NONE', #99289, 1000.000000000000227 ) ;
#55904=LINE ( 'NONE', #100810, #30589 ) ;
#55906=DIRECTION ( 'NONE',  ( -0.7071067811865486830, -0.7071067811865464625, 0.000000000000000000 ) ) ;
#55909=CARTESIAN_POINT ( 'NONE',  ( 1.499999999999996225, -4.912538124160712449, 4.000000000000000000 ) ) ;
#55910=VERTEX_POINT ( 'NONE', #15398 ) ;
#55911=EDGE_CURVE ( 'NONE', #6161, #14902, #114033, .T. ) ;
#55912=ORIENTED_EDGE ( 'NONE', *, *, #132742, .F. ) ;
#55914=ORIENTED_EDGE ( 'NONE', *, *, #99097, .T. ) ;
#55916=CARTESIAN_POINT ( 'NONE',  ( -14.99451991528749595, 28.92564299267948513, 4.000000000000000000 ) ) ;
#55917=ORIENTED_EDGE ( 'NONE', *, *, #793, .F. ) ;
#55918=CARTESIAN_POINT ( 'NONE',  ( -34.91107144025656339, 21.84219451764876396, 4.000000000000000000 ) ) ;
#55919=LINE ( 'NONE', #89243, #91818 ) ;
#55920=VECTOR ( 'NONE', #135681, 1000.000000000000000 ) ;
#55922=FACE_OUTER_BOUND ( 'NONE', #126928, .T. ) ;
#55923=ADVANCED_FACE ( 'NONE', ( #24881 ), #80029, .F. ) ;
#55924=FACE_BOUND ( 'NONE', #50090, .T. ) ;
#55925=ORIENTED_EDGE ( 'NONE', *, *, #85267, .T. ) ;
#55926=CARTESIAN_POINT ( 'NONE',  ( -3.299744871391591339, -27.71228299555208352, 4.000000000000000000 ) ) ;
#55927=ADVANCED_FACE ( 'NONE', ( #89426 ), #113306, .F. ) ;
#55928=LINE ( 'NONE', #100832, #55436 ) ;
#55929=EDGE_CURVE ( 'NONE', #23492, #27958, #59681, .T. ) ;
#55930=CARTESIAN_POINT ( 'NONE',  ( -34.92500000000001137, 22.22500000000000142, 4.000000000000000000 ) ) ;
#55931=DIRECTION ( 'NONE',  ( 0.7071067811865486830, -0.7071067811865464625, -0.000000000000000000 ) ) ;
#55932=EDGE_LOOP ( 'NONE', ( #57464, #130674, #66089, #121781 ) ) ;
#55933=CARTESIAN_POINT ( 'NONE',  ( 18.48921356237309510, -27.52281430457068367, 5.000000000000000000 ) ) ;
#55935=VERTEX_POINT ( 'NONE', #3121 ) ;
#55936=ORIENTED_EDGE ( 'NONE', *, *, #112084, .F. ) ;
#55937=EDGE_CURVE ( 'NONE', #77443, #133096, #47411, .T. ) ;
#55938=EDGE_CURVE ( 'NONE', #64078, #142188, #45257, .T. ) ;
#55940=ORIENTED_EDGE ( 'NONE', *, *, #24077, .F. ) ;
#55941=DIRECTION ( 'NONE',  ( -0.7071067811865486830, -0.7071067811865464625, 0.000000000000000000 ) ) ;
#55942=ADVANCED_FACE ( 'NONE', ( #34339 ), #103158, .T. ) ;
#55943=CARTESIAN_POINT ( 'NONE',  ( -32.99451991528749062, 28.92564299267960948, 4.000000000000000000 ) ) ;
#55944=ORIENTED_EDGE ( 'NONE', *, *, #10881, .T. ) ;
#55945=CARTESIAN_POINT ( 'NONE',  ( -36.18398860626899705, 28.73617430169812437, 5.000000000000000000 ) ) ;
#55946=CARTESIAN_POINT ( 'NONE',  ( -11.56319896779163159, -12.74070752338414891, 9.898150129686403176 ) ) ;
#55947=AXIS2_PLACEMENT_3D ( 'NONE', #67960, #33184, #25100 ) ;
#55948=( BOUNDED_CURVE ( )  B_SPLINE_CURVE ( 3, ( #111760, #37778, #137079, #48644 ),
 .UNSPECIFIED., .F., .F. ) 
 B_SPLINE_CURVE_WITH_KNOTS ( ( 4, 4 ),
 ( 5.106027341939290309, 6.645403452391243526 ),
 .UNSPECIFIED. ) 
 CURVE ( )  GEOMETRIC_REPRESENTATION_ITEM ( )  RATIONAL_B_SPLINE_CURVE ( ( 1.000000000000000000, 0.8120851936182305053, 0.8120851936182305053, 1.000000000000000000 ) ) 
 REPRESENTATION_ITEM ( '' )  );
#55950=EDGE_CURVE ( 'NONE', #113151, #36832, #135796, .T. ) ;
#55951=AXIS2_PLACEMENT_3D ( 'NONE', #6098, #127948, #92418 ) ;
#55952=CARTESIAN_POINT ( 'NONE',  ( -33.48921356237309510, -27.52281430457078670, 5.000000000000000000 ) ) ;
#55953=FACE_OUTER_BOUND ( 'NONE', #23582, .T. ) ;
#55954=DIRECTION ( 'NONE',  ( -0.6830127018922180770, -0.6830127018922204085, -0.2588190451025213501 ) ) ;
#55955=CARTESIAN_POINT ( 'NONE',  ( -30.29974487139158867, -27.71228299555227537, 4.000000000000000000 ) ) ;
#55957=ORIENTED_EDGE ( 'NONE', *, *, #77766, .F. ) ;
#55958=EDGE_LOOP ( 'NONE', ( #15599, #63726, #124141, #54735 ) ) ;
#55959=VECTOR ( 'NONE', #87538, 1000.000000000000000 ) ;
#55960=AXIS2_PLACEMENT_3D ( 'NONE', #33920, #9244, #131797 ) ;
#55961=EDGE_LOOP ( 'NONE', ( #89387, #137964, #46615 ) ) ;
#55962=VECTOR ( 'NONE', #143353, 1000.000000000000000 ) ;
#55963=ORIENTED_EDGE ( 'NONE', *, *, #3303, .F. ) ;
#55965=LINE ( 'NONE', #22553, #35795 ) ;
#55966=EDGE_CURVE ( 'NONE', #106022, #135463, #56854, .T. ) ;
#55970=VERTEX_POINT ( 'NONE', #95125 ) ;
#55972=CARTESIAN_POINT ( 'NONE',  ( -81.18398860626899705, 28.73617430169844056, 5.000000000000000000 ) ) ;
#55973=LINE ( 'NONE', #91435, #30049 ) ;
#55974=ORIENTED_EDGE ( 'NONE', *, *, #72695, .T. ) ;
#55976=DIRECTION ( 'NONE',  ( -0.3543493200069162685, -0.000000000000000000, -0.9351131265310288487 ) ) ;
#55977=ADVANCED_FACE ( 'NONE', ( #49534 ), #106697, .F. ) ;
#55978=LINE ( 'NONE', #142264, #132440 ) ;
#55980=LINE ( 'NONE', #24037, #16003 ) ;
#55983=DIRECTION ( 'NONE',  ( 0.7071067811865487940, 0.7071067811865463515, -0.000000000000000000 ) ) ;
#55984=ADVANCED_FACE ( 'NONE', ( #84299 ), #5951, .F. ) ;
#55985=DIRECTION ( 'NONE',  ( 0.7071067811865486830, -0.7071067811865464625, -0.000000000000000000 ) ) ;
#55986=DIRECTION ( 'NONE',  ( -0.6830127018922180770, -0.6830127018922204085, -0.2588190451025213501 ) ) ;
#55988=PLANE ( 'NONE',  #101779 ) ;
#55989=ORIENTED_EDGE ( 'NONE', *, *, #140213, .T. ) ;
#55990=CARTESIAN_POINT ( 'NONE',  ( 24.45983838949724998, 18.75929247661552779, 8.305906642995541489 ) ) ;
#55991=CARTESIAN_POINT ( 'NONE',  ( -36.18398860626899705, 28.73617430169812437, 5.000000000000000000 ) ) ;
#55992=PLANE ( 'NONE',  #107385 ) ;
#55994=VECTOR ( 'NONE', #17381, 1000.000000000000227 ) ;
#55995=ADVANCED_FACE ( 'NONE', ( #62532 ), #29166, .F. ) ;
#55996=LINE ( 'NONE', #100195, #96870 ) ;
#55998=EDGE_CURVE ( 'NONE', #52228, #18107, #137948, .T. ) ;
#56000=CARTESIAN_POINT ( 'NONE',  ( 0.000000000000000000, 0.000000000000000000, 5.000000000000000000 ) ) ;
#56001=DIRECTION ( 'NONE',  ( -0.7071067811865486830, 0.7071067811865464625, 0.000000000000000000 ) ) ;
#56002=ORIENTED_EDGE ( 'NONE', *, *, #37781, .T. ) ;
#56004=CARTESIAN_POINT ( 'NONE',  ( -27.79289321881325847, 9.759292476615621936, 5.000000000000000000 ) ) ;
#56005=EDGE_CURVE ( 'NONE', #41034, #15918, #40774, .T. ) ;
#56006=VERTEX_POINT ( 'NONE', #19004 ) ;
#56007=DIRECTION ( 'NONE',  ( 0.7071067811865486830, -0.7071067811865464625, -0.000000000000000000 ) ) ;
#56008=CARTESIAN_POINT ( 'NONE',  ( 3.299744871391591339, -27.71228299555208352, 4.000000000000000000 ) ) ;
#56009=EDGE_LOOP ( 'NONE', ( #124794, #101011, #142350, #56106 ) ) ;
#56010=ORIENTED_EDGE ( 'NONE', *, *, #91930, .T. ) ;
#56011=LINE ( 'NONE', #56739, #35727 ) ;
#56012=CARTESIAN_POINT ( 'NONE',  ( -18.79289321881332597, -20.24070752338407431, 5.000000000000000000 ) ) ;
#56013=AXIS2_PLACEMENT_3D ( 'NONE', #133663, #46706, #23454 ) ;
#56014=VERTEX_POINT ( 'NONE', #84977 ) ;
#56015=CARTESIAN_POINT ( 'NONE',  ( 6.005480084712508493, 28.92564299267933947, 4.000000000000000000 ) ) ;
#56016=CARTESIAN_POINT ( 'NONE',  ( -11.81601139373100651, 28.73617430169779041, 5.000000000000000000 ) ) ;
#56017=FACE_OUTER_BOUND ( 'NONE', #137414, .T. ) ;
#56018=ORIENTED_EDGE ( 'NONE', *, *, #45438, .T. ) ;
#56019=EDGE_CURVE ( 'NONE', #107142, #18858, #129179, .T. ) ;
#56021=CARTESIAN_POINT ( 'NONE',  ( 17.01088028653936135, -22.02621442084248571, 4.990779571109217549 ) ) ;
#56023=VECTOR ( 'NONE', #24485, 1000.000000000000000 ) ;
#56024=DIRECTION ( 'NONE',  ( -0.000000000000000000, -0.3543493200069152693, 0.9351131265310292928 ) ) ;
#56025=AXIS2_PLACEMENT_3D ( 'NONE', #37083, #104475, #49431 ) ;
#56028=EDGE_CURVE ( 'NONE', #105421, #14025, #7391, .T. ) ;
#56029=LINE ( 'NONE', #79221, #115961 ) ;
#56030=ORIENTED_EDGE ( 'NONE', *, *, #15723, .T. ) ;
#56031=ORIENTED_EDGE ( 'NONE', *, *, #56033, .T. ) ;
#56033=EDGE_CURVE ( 'NONE', #133992, #56202, #74107, .T. ) ;
#56034=ORIENTED_EDGE ( 'NONE', *, *, #90893, .T. ) ;
#56036=VECTOR ( 'NONE', #122640, 1000.000000000000000 ) ;
#56037=CARTESIAN_POINT ( 'NONE',  ( 4.980122250714494214, -17.24070752338410273, 20.23474786156470628 ) ) ;
#56038=CARTESIAN_POINT ( 'NONE',  ( -7.171830600776411657, -14.24070752338413648, 4.000000000000000000 ) ) ;
#56039=ORIENTED_EDGE ( 'NONE', *, *, #130402, .T. ) ;
#56040=LINE ( 'NONE', #100231, #71730 ) ;
#56043=EDGE_CURVE ( 'NONE', #80281, #63122, #61824, .T. ) ;
#56044=DIRECTION ( 'NONE',  ( -0.000000000000000000, -0.3543493200069152693, 0.9351131265310292928 ) ) ;
#56046=EDGE_LOOP ( 'NONE', ( #56542, #96669, #137540, #32237 ) ) ;
#56048=DIRECTION ( 'NONE',  ( 0.3543493200069162685, -0.000000000000000000, -0.9351131265310288487 ) ) ;
#56050=CARTESIAN_POINT ( 'NONE',  ( 5.816011393731002066, 28.73617430169783304, 5.000000000000000000 ) ) ;
#56051=VECTOR ( 'NONE', #36063, 1000.000000000000000 ) ;
#56054=CARTESIAN_POINT ( 'NONE',  ( 34.49999999999975842, 6.054329344830883031, 4.994342998332162331 ) ) ;
#56055=DIRECTION ( 'NONE',  ( 0.7071067811865487940, -0.7071067811865463515, 0.000000000000000000 ) ) ;
#56057=DIRECTION ( 'NONE',  ( 0.6830127018922181881, 0.6830127018922202975, -0.2588190451025214056 ) ) ;
#56058=DIRECTION ( 'NONE',  ( 0.6830127018922181881, 0.6830127018922202975, -0.2588190451025214056 ) ) ;
#56059=ORIENTED_EDGE ( 'NONE', *, *, #30675, .F. ) ;
#56060=VERTEX_POINT ( 'NONE', #38626 ) ;
#56062=DIRECTION ( 'NONE',  ( 0.7071067811865486830, -0.7071067811865464625, -0.000000000000000000 ) ) ;
#56063=LINE ( 'NONE', #55327, #60015 ) ;
#56066=VECTOR ( 'NONE', #70443, 1000.000000000000000 ) ;
#56067=CARTESIAN_POINT ( 'NONE',  ( -19.49999999999985789, 5.696342897626483825, -7.587980461218443828 ) ) ;
#56068=EDGE_CURVE ( 'NONE', #2946, #53913, #39355, .T. ) ;
#56072=ADVANCED_FACE ( 'NONE', ( #28474 ), #72736, .F. ) ;
#56080=CARTESIAN_POINT ( 'NONE',  ( -13.49999999999989875, -10.53360074219763121, 5.000000000000000000 ) ) ;
#56081=PLANE ( 'NONE',  #54640 ) ;
#56083=DIRECTION ( 'NONE',  ( -0.6830127018922180770, -0.6830127018922204085, -0.2588190451025213501 ) ) ;
#56085=EDGE_CURVE ( 'NONE', #23517, #115243, #116887, .T. ) ;
#56086=DIRECTION ( 'NONE',  ( 1.000000000000000000, 0.000000000000000000, 0.000000000000000000 ) ) ;
#56087=VERTEX_POINT ( 'NONE', #5250 ) ;
#56088=CARTESIAN_POINT ( 'NONE',  ( -4.499999999999966249, -7.533600742197664069, 5.000000000000000000 ) ) ;
#56089=FACE_OUTER_BOUND ( 'NONE', #120597, .T. ) ;
#56090=DIRECTION ( 'NONE',  ( -0.7071067811865486830, 0.7071067811865464625, 0.000000000000000000 ) ) ;
#56091=CARTESIAN_POINT ( 'NONE',  ( -34.45011844616455221, -20.99769585840582664, 5.000000000000000888 ) ) ;
#56092=PLANE ( 'NONE',  #48588 ) ;
#56093=CARTESIAN_POINT ( 'NONE',  ( -15.79289321881334551, 9.759292476615621936, 5.000000000000000000 ) ) ;
#56094=ORIENTED_EDGE ( 'NONE', *, *, #2628, .T. ) ;
#56095=LINE ( 'NONE', #123491, #131067 ) ;
#56097=DIRECTION ( 'NONE',  ( -0.3543493200069162685, -0.000000000000000000, -0.9351131265310288487 ) ) ;
#56098=FACE_OUTER_BOUND ( 'NONE', #23169, .T. ) ;
#56099=PLANE ( 'NONE',  #15545 ) ;
#56100=EDGE_LOOP ( 'NONE', ( #5074, #129383, #135645, #99938 ) ) ;
#56101=LINE ( 'NONE', #69832, #88709 ) ;
#56102=EDGE_LOOP ( 'NONE', ( #118560, #57854, #23354, #26820 ) ) ;
#56103=AXIS2_PLACEMENT_3D ( 'NONE', #23819, #47747, #79679 ) ;
#56104=VECTOR ( 'NONE', #117549, 1000.000000000000000 ) ;
#56106=ORIENTED_EDGE ( 'NONE', *, *, #114142, .F. ) ;
#56108=DIRECTION ( 'NONE',  ( 0.7071067811865487940, 0.7071067811865463515, -0.000000000000000000 ) ) ;
#56110=DIRECTION ( 'NONE',  ( 0.7071067811865487940, 0.7071067811865463515, 0.000000000000000000 ) ) ;
#56112=DIRECTION ( 'NONE',  ( 0.7071067811865487940, 0.7071067811865463515, 0.000000000000000000 ) ) ;
#56113=FACE_BOUND ( 'NONE', #89153, .T. ) ;
#56114=CARTESIAN_POINT ( 'NONE',  ( 26.99999999999981526, -5.527737879153164613, -7.983877177622434651 ) ) ;
#56115=ADVANCED_FACE ( 'NONE', ( #50935 ), #104587, .F. ) ;
#56116=EDGE_CURVE ( 'NONE', #45742, #87036, #20407, .T. ) ;
#56117=DIRECTION ( 'NONE',  ( -0.6830127018922180770, -0.6830127018922204085, -0.2588190451025213501 ) ) ;
#56118=CARTESIAN_POINT ( 'NONE',  ( -45.29974487139158867, -27.71228299555237840, 4.000000000000000000 ) ) ;
#56120=EDGE_LOOP ( 'NONE', ( #142056, #28248, #100970, #62695 ) ) ;
#56121=VECTOR ( 'NONE', #102997, 1000.000000000000000 ) ;
#56122=LINE ( 'NONE', #65575, #99533 ) ;
#56123=ORIENTED_EDGE ( 'NONE', *, *, #39123, .F. ) ;
#56124=ADVANCED_FACE ( 'NONE', ( #87828 ), #85673, .F. ) ;
#56125=EDGE_CURVE ( 'NONE', #135598, #78218, #110270, .T. ) ;
#56126=ORIENTED_EDGE ( 'NONE', *, *, #23214, .F. ) ;
#56130=EDGE_CURVE ( 'NONE', #55125, #58070, #52340, .T. ) ;
#56131=CARTESIAN_POINT ( 'NONE',  ( 0.1839886062690032631, 28.73617430169787568, 5.000000000000000000 ) ) ;
#56132=ADVANCED_FACE ( 'NONE', ( #96529 ), #74847, .F. ) ;
#56133=AXIS2_PLACEMENT_3D ( 'NONE', #64088, #44513, #66244 ) ;
#56135=LINE ( 'NONE', #974, #102364 ) ;
#56137=EDGE_CURVE ( 'NONE', #127061, #70950, #132803, .T. ) ;
#56138=CARTESIAN_POINT ( 'NONE',  ( 4.499999999999973355, 18.43112307739199451, 4.000000000000000000 ) ) ;
#56140=EDGE_CURVE ( 'NONE', #34231, #129574, #55210, .T. ) ;
#56141=CARTESIAN_POINT ( 'NONE',  ( -24.61500991739762512, 5.335133370053846136, 4.556819239218478756 ) ) ;
#56142=LINE ( 'NONE', #47420, #131581 ) ;
#56143=CARTESIAN_POINT ( 'NONE',  ( -34.49999999999975842, 21.05432934483072671, 4.994342998332167660 ) ) ;
#56144=DIRECTION ( 'NONE',  ( 0.7071067811865486830, -0.7071067811865464625, -0.000000000000000000 ) ) ;
#56145=DIRECTION ( 'NONE',  ( 0.7071067811865487940, 0.7071067811865463515, 0.000000000000000000 ) ) ;
#56146=VERTEX_POINT ( 'NONE', #76992 ) ;
#56147=AXIS2_PLACEMENT_3D ( 'NONE', #95726, #62409, #65274 ) ;
#56149=VERTEX_POINT ( 'NONE', #66099 ) ;
#56150=DIRECTION ( 'NONE',  ( 0.7071067811865487940, 0.7071067811865463515, -0.000000000000000000 ) ) ;
#56151=CARTESIAN_POINT ( 'NONE',  ( 36.18398860626899705, 28.73617430169812437, 5.000000000000000000 ) ) ;
#56152=ORIENTED_EDGE ( 'NONE', *, *, #133178, .T. ) ;
#56153=ADVANCED_FACE ( 'NONE', ( #41457 ), #76251, .F. ) ;
#56154=EDGE_LOOP ( 'NONE', ( #100137, #131798, #44565, #43494 ) ) ;
#56155=ORIENTED_EDGE ( 'NONE', *, *, #136480, .F. ) ;
#56157=VECTOR ( 'NONE', #97931, 999.9999999999998863 ) ;
#56158=ORIENTED_EDGE ( 'NONE', *, *, #136468, .F. ) ;
#56159=CARTESIAN_POINT ( 'NONE',  ( 34.42499999999998295, 20.97718569542917777, 5.000000000000000000 ) ) ;
#56160=( BOUNDED_CURVE ( )  B_SPLINE_CURVE ( 3, ( #135040, #79953, #58930, #103092 ),
 .UNSPECIFIED., .F., .T. ) 
 B_SPLINE_CURVE_WITH_KNOTS ( ( 4, 4 ),
 ( 5.005968288816728951, 5.074607125596344304 ),
 .UNSPECIFIED. ) 
 CURVE ( )  GEOMETRIC_REPRESENTATION_ITEM ( )  RATIONAL_B_SPLINE_CURVE ( ( 1.000000000000000000, 0.9996074310407763175, 0.9996074310407763175, 1.000000000000000000 ) ) 
 REPRESENTATION_ITEM ( '' )  );
#56161=ADVANCED_FACE ( 'NONE', ( #65399 ), #141504, .F. ) ;
#56162=DIRECTION ( 'NONE',  ( 0.3543493200069162685, -0.000000000000000000, -0.9351131265310288487 ) ) ;
#56165=ORIENTED_EDGE ( 'NONE', *, *, #41196, .F. ) ;
#56167=DIRECTION ( 'NONE',  ( -0.7071067811865486830, -0.7071067811865464625, 0.000000000000000000 ) ) ;
#56168=DIRECTION ( 'NONE',  ( -0.7071067811865487940, 0.7071067811865463515, -0.000000000000000000 ) ) ;
#56169=VECTOR ( 'NONE', #40497, 1000.000000000000227 ) ;
#56170=VECTOR ( 'NONE', #65252, 1000.000000000000000 ) ;
#56171=CARTESIAN_POINT ( 'NONE',  ( -14.20710678118644132, -5.240707523384227073, 5.000000000000000000 ) ) ;
#56172=ORIENTED_EDGE ( 'NONE', *, *, #121168, .F. ) ;
#56174=ORIENTED_EDGE ( 'NONE', *, *, #35715, .T. ) ;
#56175=CARTESIAN_POINT ( 'NONE',  ( 2.510786437626908008, -27.52281430457053446, 5.000000000000000000 ) ) ;
#56176=DIRECTION ( 'NONE',  ( -0.000000000000000000, 0.3543493200069153248, 0.9351131265310292928 ) ) ;
#56177=VECTOR ( 'NONE', #127085, 1000.000000000000000 ) ;
#56178=LINE ( 'NONE', #24225, #40165 ) ;
#56179=ORIENTED_EDGE ( 'NONE', *, *, #133295, .T. ) ;
#56181=EDGE_CURVE ( 'NONE', #118712, #80915, #119710, .T. ) ;
#56182=LINE ( 'NONE', #84661, #138275 ) ;
#56183=ORIENTED_EDGE ( 'NONE', *, *, #54, .T. ) ;
#56184=EDGE_CURVE ( 'NONE', #72338, #103200, #119024, .T. ) ;
#56186=PLANE ( 'NONE',  #107303 ) ;
#56190=LINE ( 'NONE', #10472, #63250 ) ;
#56191=EDGE_CURVE ( 'NONE', #100333, #138017, #108836, .T. ) ;
#56192=DIRECTION ( 'NONE',  ( 0.7071067811865487940, 0.7071067811865463515, 0.000000000000000000 ) ) ;
#56193=DIRECTION ( 'NONE',  ( 0.3543493200069162685, -0.000000000000000000, -0.9351131265310288487 ) ) ;
#56194=CARTESIAN_POINT ( 'NONE',  ( -33.18398860626899705, 28.73617430169810305, 5.000000000000000000 ) ) ;
#56195=ORIENTED_EDGE ( 'NONE', *, *, #137048, .F. ) ;
#56197=DIRECTION ( 'NONE',  ( -0.7071067811865486830, -0.7071067811865464625, -0.000000000000000000 ) ) ;
#56199=ADVANCED_FACE ( 'NONE', ( #107436 ), #42207, .T. ) ;
#56200=CARTESIAN_POINT ( 'NONE',  ( -8.999999999999941380, -4.068876922607777225, 4.000000000000000000 ) ) ;
#56201=FACE_OUTER_BOUND ( 'NONE', #2282, .T. ) ;
#56202=VERTEX_POINT ( 'NONE', #86424 ) ;
#56204=FACE_OUTER_BOUND ( 'NONE', #60020, .T. ) ;
#56205=CARTESIAN_POINT ( 'NONE',  ( 6.489213562373093325, -27.52281430457059841, 5.000000000000000000 ) ) ;
#56206=CARTESIAN_POINT ( 'NONE',  ( -26.99999999999980105, 1.552185695429149304, 5.000000000000000000 ) ) ;
#56207=ORIENTED_EDGE ( 'NONE', *, *, #41668, .T. ) ;
#56208=EDGE_CURVE ( 'NONE', #142584, #137698, #10946, .T. ) ;
#56209=DIRECTION ( 'NONE',  ( -0.7071067811865487940, 0.7071067811865463515, -0.000000000000000000 ) ) ;
#56210=DIRECTION ( 'NONE',  ( 0.7071067811865486830, -0.7071067811865464625, -0.000000000000000000 ) ) ;
#56211=LINE ( 'NONE', #112678, #37654 ) ;
#56212=CARTESIAN_POINT ( 'NONE',  ( 6.489213562373093325, -27.52281430457059841, 5.000000000000000000 ) ) ;
#56214=VECTOR ( 'NONE', #60599, 1000.000000000000227 ) ;
#56215=DIRECTION ( 'NONE',  ( 0.6830127018922181881, 0.6830127018922202975, -0.2588190451025214056 ) ) ;
#56216=DIRECTION ( 'NONE',  ( 0.7071067811865487940, 0.7071067811865463515, 0.000000000000000000 ) ) ;
#56218=ADVANCED_FACE ( 'NONE', ( #9521 ), #97998, .F. ) ;
#56219=VECTOR ( 'NONE', #104807, 1000.000000000000000 ) ;
#56220=EDGE_LOOP ( 'NONE', ( #25182, #28241, #117112, #45539 ) ) ;
#56222=ORIENTED_EDGE ( 'NONE', *, *, #15930, .T. ) ;
#56223=AXIS2_PLACEMENT_3D ( 'NONE', #133614, #55338, #74967 ) ;
#56225=VECTOR ( 'NONE', #73021, 1000.000000000000227 ) ;
#56226=PLANE ( 'NONE',  #113187 ) ;
#56227=CARTESIAN_POINT ( 'NONE',  ( 5.488313940715645600, 6.759292476615645917, 16.35960578974468049 ) ) ;
#56228=DIRECTION ( 'NONE',  ( -0.7071067811865486830, -0.7071067811865464625, 0.000000000000000000 ) ) ;
#56229=EDGE_CURVE ( 'NONE', #44279, #19888, #42921, .T. ) ;
#56230=DIRECTION ( 'NONE',  ( -0.000000000000000000, -0.3543493200069152693, 0.9351131265310292928 ) ) ;
#56231=FACE_OUTER_BOUND ( 'NONE', #106539, .T. ) ;
#56232=ORIENTED_EDGE ( 'NONE', *, *, #93656, .T. ) ;
#56234=ORIENTED_EDGE ( 'NONE', *, *, #62243, .T. ) ;
#56235=CARTESIAN_POINT ( 'NONE',  ( 4.499999999999974243, -7.912538124160676922, 4.000000000000000000 ) ) ;
#56236=DIRECTION ( 'NONE',  ( -0.7071067811865486830, -0.7071067811865464625, 0.000000000000000000 ) ) ;
#56242=ADVANCED_FACE ( 'NONE', ( #13102 ), #89950, .F. ) ;
#56243=CARTESIAN_POINT ( 'NONE',  ( -32.99999999999976552, -8.731860332648864187, -2.120594902707616747 ) ) ;
#56244=ORIENTED_EDGE ( 'NONE', *, *, #23147, .T. ) ;
#56246=CARTESIAN_POINT ( 'NONE',  ( -31.17183060077626067, 6.759292476615656575, 4.000000000000000000 ) ) ;
#56247=DIRECTION ( 'NONE',  ( 0.7071067811865486830, -0.7071067811865464625, -0.000000000000000000 ) ) ;
#56248=LINE ( 'NONE', #35188, #12696 ) ;
#56249=VECTOR ( 'NONE', #50200, 1000.000000000000000 ) ;
#56250=VECTOR ( 'NONE', #46063, 1000.000000000000000 ) ;
#56253=PLANE ( 'NONE',  #65277 ) ;
#56254=ORIENTED_EDGE ( 'NONE', *, *, #18418, .F. ) ;
#56255=EDGE_CURVE ( 'NONE', #139810, #5145, #36314, .T. ) ;
#56256=CARTESIAN_POINT ( 'NONE',  ( -31.49999999999977973, 22.22500000000000142, 4.362957392718792349 ) ) ;
#56258=VERTEX_POINT ( 'NONE', #56683 ) ;
#56259=ORIENTED_EDGE ( 'NONE', *, *, #37425, .F. ) ;
#56262=DIRECTION ( 'NONE',  ( -0.000000000000000000, 0.3543493200069153248, 0.9351131265310292928 ) ) ;
#56263=PLANE ( 'NONE',  #79069 ) ;
#56264=LINE ( 'NONE', #133779, #60229 ) ;
#56265=EDGE_CURVE ( 'NONE', #103031, #36832, #123341, .T. ) ;
#56266=CARTESIAN_POINT ( 'NONE',  ( 26.14818355038129027, 17.25929247661554200, 8.802941693769263054 ) ) ;
#56267=FACE_OUTER_BOUND ( 'NONE', #87798, .T. ) ;
#56268=ORIENTED_EDGE ( 'NONE', *, *, #11820, .T. ) ;
#56271=VECTOR ( 'NONE', #12160, 1000.000000000000000 ) ;
#56272=PLANE ( 'NONE',  #116543 ) ;
#56274=VERTEX_POINT ( 'NONE', #91414 ) ;
#56276=ORIENTED_EDGE ( 'NONE', *, *, #10941, .T. ) ;
#56278=DIRECTION ( 'NONE',  ( 0.7071067811865487940, 0.7071067811865463515, 0.000000000000000000 ) ) ;
#56279=CARTESIAN_POINT ( 'NONE',  ( -0.4892135623730947680, -27.52281430457055578, 5.000000000000000000 ) ) ;
#56280=CARTESIAN_POINT ( 'NONE',  ( -15.48921356237309510, -27.52281430457066236, 5.000000000000000000 ) ) ;
#56281=DIRECTION ( 'NONE',  ( -0.7071067811865486830, -0.7071067811865464625, -0.000000000000000000 ) ) ;
#56283=ORIENTED_EDGE ( 'NONE', *, *, #20282, .F. ) ;
#56284=VECTOR ( 'NONE', #87883, 1000.000000000000000 ) ;
#56285=DIRECTION ( 'NONE',  ( -0.7071067811865486830, -0.7071067811865464625, 0.000000000000000000 ) ) ;
#56288=ORIENTED_EDGE ( 'NONE', *, *, #30698, .F. ) ;
#56291=CARTESIAN_POINT ( 'NONE',  ( -34.49999999999975842, -5.945670655168998842, 4.994342998332166772 ) ) ;
#56293=VECTOR ( 'NONE', #115705, 999.9999999999998863 ) ;
#56296=FACE_BOUND ( 'NONE', #76089, .T. ) ;
#56297=DIRECTION ( 'NONE',  ( -0.7071067811865487940, 0.7071067811865463515, 0.000000000000000000 ) ) ;
#56298=DIRECTION ( 'NONE',  ( 0.7071067811865487940, 0.7071067811865463515, 0.000000000000000000 ) ) ;
#56299=LINE ( 'NONE', #68578, #25087 ) ;
#56300=LINE ( 'NONE', #134548, #4041 ) ;
#56302=ORIENTED_EDGE ( 'NONE', *, *, #124514, .T. ) ;
#56303=ADVANCED_FACE ( 'NONE', ( #133489 ), #110977, .F. ) ;
#56304=VECTOR ( 'NONE', #6720, 1000.000000000000000 ) ;
#56305=ORIENTED_EDGE ( 'NONE', *, *, #47966, .F. ) ;
#56307=ORIENTED_EDGE ( 'NONE', *, *, #96225, .F. ) ;
#56308=EDGE_CURVE ( 'NONE', #125435, #132154, #34175, .T. ) ;
#56310=VERTEX_POINT ( 'NONE', #58099 ) ;
#56311=ADVANCED_FACE ( 'NONE', ( #102993 ), #100145, .F. ) ;
#56312=PLANE ( 'NONE',  #100183 ) ;
#56313=ADVANCED_FACE ( 'NONE', ( #47929 ), #92093, .F. ) ;
#56314=AXIS2_PLACEMENT_3D ( 'NONE', #68107, #79704, #25986 ) ;
#56315=DIRECTION ( 'NONE',  ( 0.000000000000000000, -1.000000000000000000, 0.000000000000000000 ) ) ;
#56316=LINE ( 'NONE', #55568, #791 ) ;
#56317=ORIENTED_EDGE ( 'NONE', *, *, #68076, .T. ) ;
#56318=LINE ( 'NONE', #135285, #83165 ) ;
#56319=PLANE ( 'NONE',  #38037 ) ;
#56320=DIRECTION ( 'NONE',  ( -0.7071067811865486830, -0.7071067811865464625, -0.000000000000000000 ) ) ;
#56321=VECTOR ( 'NONE', #23505, 999.9999999999998863 ) ;
#56322=EDGE_CURVE ( 'NONE', #112494, #120574, #22537, .T. ) ;
#56323=DIRECTION ( 'NONE',  ( -0.7071067811865486830, -0.7071067811865464625, -0.000000000000000000 ) ) ;
#56324=CARTESIAN_POINT ( 'NONE',  ( -15.41161490594820904, 22.22500000000000142, 4.777194822843812361 ) ) ;
#56325=CARTESIAN_POINT ( 'NONE',  ( -12.48921356237309155, -27.52281430457064104, 5.000000000000000000 ) ) ;
#56326=DIRECTION ( 'NONE',  ( -0.3543493200069162685, -0.000000000000000000, -0.9351131265310288487 ) ) ;
#56327=VERTEX_POINT ( 'NONE', #78391 ) ;
#56330=ADVANCED_FACE ( 'NONE', ( #68963 ), #122584, .F. ) ;
#56334=VERTEX_POINT ( 'NONE', #2201 ) ;
#56339=DIRECTION ( 'NONE',  ( 0.7071067811865487940, 0.7071067811865463515, -0.000000000000000000 ) ) ;
#56344=ORIENTED_EDGE ( 'NONE', *, *, #2950, .F. ) ;
#56345=VECTOR ( 'NONE', #128500, 1000.000000000000000 ) ;
#56347=CARTESIAN_POINT ( 'NONE',  ( 11.90156419391756337, 11.25929247661560595, 10.79108189686409780 ) ) ;
#56348=AXIS2_PLACEMENT_3D ( 'NONE', #72477, #138402, #47862 ) ;
#56349=DIRECTION ( 'NONE',  ( 0.7071067811865487940, 0.7071067811865463515, -0.000000000000000000 ) ) ;
#56352=CARTESIAN_POINT ( 'NONE',  ( -3.707106781186522593, 20.25929247661551358, 5.000000000000000000 ) ) ;
#56353=ORIENTED_EDGE ( 'NONE', *, *, #62865, .T. ) ;
#56354=CARTESIAN_POINT ( 'NONE',  ( 20.29298673570680123, -21.74070752338406720, 4.999753212805221558 ) ) ;
#56355=ORIENTED_EDGE ( 'NONE', *, *, #70554, .F. ) ;
#56356=ORIENTED_EDGE ( 'NONE', *, *, #110847, .T. ) ;
#56357=ORIENTED_EDGE ( 'NONE', *, *, #57735, .F. ) ;
#56358=EDGE_CURVE ( 'NONE', #31963, #137771, #135627, .T. ) ;
#56359=AXIS2_PLACEMENT_3D ( 'NONE', #24779, #24081, #68340 ) ;
#56360=LINE ( 'NONE', #112133, #123350 ) ;
#56361=FACE_OUTER_BOUND ( 'NONE', #44756, .T. ) ;
#56362=CARTESIAN_POINT ( 'NONE',  ( 18.18398860626898994, 28.73617430169800002, 5.000000000000000000 ) ) ;
#56363=AXIS2_PLACEMENT_3D ( 'NONE', #115550, #93838, #6782 ) ;
#56364=EDGE_LOOP ( 'NONE', ( #49096, #142799, #139356, #42692 ) ) ;
#56365=DIRECTION ( 'NONE',  ( 1.000000000000000000, 0.000000000000000000, 0.000000000000000000 ) ) ;
#56366=EDGE_CURVE ( 'NONE', #112045, #141891, #79135, .T. ) ;
#56369=DIRECTION ( 'NONE',  ( -0.7071067811865486830, -0.7071067811865464625, 0.000000000000000000 ) ) ;
#56370=PLANE ( 'NONE',  #44361 ) ;
#56371=ORIENTED_EDGE ( 'NONE', *, *, #76655, .T. ) ;
#56372=VERTEX_POINT ( 'NONE', #124034 ) ;
#56373=EDGE_CURVE ( 'NONE', #48791, #94433, #113132, .T. ) ;
#56374=ORIENTED_EDGE ( 'NONE', *, *, #2999, .T. ) ;
#56375=PLANE ( 'NONE',  #44152 ) ;
#56377=VECTOR ( 'NONE', #4932, 1000.000000000000000 ) ;
#56378=CARTESIAN_POINT ( 'NONE',  ( 23.99999999999982592, -2.904428200921294057, -6.989807076075000403 ) ) ;
#56379=CARTESIAN_POINT ( 'NONE',  ( 27.48921356237309155, -27.52281430457074762, 5.000000000000000000 ) ) ;
#56380=CARTESIAN_POINT ( 'NONE',  ( -11.70822291016945016, -15.74070752338412404, 19.73771281079094919 ) ) ;
#56382=CARTESIAN_POINT ( 'NONE',  ( -17.99451991528748351, 28.92564299267950645, 4.000000000000000000 ) ) ;
#56383=DIRECTION ( 'NONE',  ( -0.000000000000000000, 0.3543493200069153248, 0.9351131265310292928 ) ) ;
#56384=ADVANCED_FACE ( 'NONE', ( #71812 ), #51475, .F. ) ;
#56385=CARTESIAN_POINT ( 'NONE',  ( -2.048096618150911485, 22.22500000000000142, -7.458287694568845438 ) ) ;
#56386=FACE_OUTER_BOUND ( 'NONE', #66127, .T. ) ;
#56387=ORIENTED_EDGE ( 'NONE', *, *, #83785, .F. ) ;
#56389=PLANE ( 'NONE',  #584 ) ;
#56390=EDGE_LOOP ( 'NONE', ( #37840, #67559, #49734, #125996 ) ) ;
#56392=ORIENTED_EDGE ( 'NONE', *, *, #3165, .T. ) ;
#56393=CARTESIAN_POINT ( 'NONE',  ( -1.828169399223521507, 18.75929247661552424, 4.000000000000000000 ) ) ;
#56395=EDGE_LOOP ( 'NONE', ( #98741, #46452, #121906 ) ) ;
#56396=EDGE_CURVE ( 'NONE', #1085, #63434, #39903, .T. ) ;
#56397=CARTESIAN_POINT ( 'NONE',  ( -36.48921356237310221, -27.52281430457080802, 5.000000000000000000 ) ) ;
#56398=CARTESIAN_POINT ( 'NONE',  ( -60.18398860626900415, 28.73617430169829490, 5.000000000000000000 ) ) ;
#56399=ORIENTED_EDGE ( 'NONE', *, *, #131227, .T. ) ;
#56400=LINE ( 'NONE', #54248, #34660 ) ;
#56401=VERTEX_POINT ( 'NONE', #93544 ) ;
#56402=CARTESIAN_POINT ( 'NONE',  ( -34.42500000000001137, -22.22500000000000142, 5.000000000000000000 ) ) ;
#56404=ORIENTED_EDGE ( 'NONE', *, *, #56957, .T. ) ;
#56406=DIRECTION ( 'NONE',  ( -0.6830127018922181881, 0.6830127018922202975, -0.2588190451025214056 ) ) ;
#56408=CARTESIAN_POINT ( 'NONE',  ( 10.49999999999993250, 9.052185695429077583, 5.000000000000000000 ) ) ;
#56409=VECTOR ( 'NONE', #47314, 1000.000000000000000 ) ;
#56410=VERTEX_POINT ( 'NONE', #115978 ) ;
#56411=FACE_OUTER_BOUND ( 'NONE', #6992, .T. ) ;
#56413=CARTESIAN_POINT ( 'NONE',  ( -23.67183060077630685, -0.7407075233842735917, 4.000000000000000000 ) ) ;
#56415=CARTESIAN_POINT ( 'NONE',  ( -5.510786437626906675, -27.52281430457051314, 5.000000000000000000 ) ) ;
#56416=DIRECTION ( 'NONE',  ( 0.3543493200069163240, 0.000000000000000000, 0.9351131265310288487 ) ) ;
#56417=DIRECTION ( 'NONE',  ( 0.6830127018922180770, -0.6830127018922204085, -0.2588190451025213501 ) ) ;
#56419=VECTOR ( 'NONE', #75750, 999.9999999999998863 ) ;
#56420=ORIENTED_EDGE ( 'NONE', *, *, #140373, .F. ) ;
#56421=FACE_OUTER_BOUND ( 'NONE', #78781, .T. ) ;
#56422=VERTEX_POINT ( 'NONE', #105809 ) ;
#56423=EDGE_CURVE ( 'NONE', #105277, #51650, #15927, .T. ) ;
#56424=VECTOR ( 'NONE', #22745, 1000.000000000000227 ) ;
#56425=EDGE_CURVE ( 'NONE', #69752, #65577, #18072, .T. ) ;
#56427=CARTESIAN_POINT ( 'NONE',  ( -33.48921356237309510, -27.52281430457078670, 5.000000000000000000 ) ) ;
#56428=DIRECTION ( 'NONE',  ( 0.7071067811865487940, 0.7071067811865463515, 0.000000000000000000 ) ) ;
#56430=LINE ( 'NONE', #80999, #20036 ) ;
#56431=VERTEX_POINT ( 'NONE', #95669 ) ;
#56432=DIRECTION ( 'NONE',  ( 0.6830127018922180770, -0.6830127018922204085, -0.2588190451025213501 ) ) ;
#56433=DIRECTION ( 'NONE',  ( 0.3543493200069162685, -0.000000000000000000, -0.9351131265310288487 ) ) ;
#56435=VECTOR ( 'NONE', #68639, 1000.000000000000000 ) ;
#56437=EDGE_CURVE ( 'NONE', #139662, #33976, #114562, .T. ) ;
#56438=DIRECTION ( 'NONE',  ( 1.000000000000000000, 0.000000000000000000, 0.000000000000000000 ) ) ;
#56439=ADVANCED_FACE ( 'NONE', ( #104400 ), #103667, .F. ) ;
#56440=CARTESIAN_POINT ( 'NONE',  ( 9.792893218813395251, -8.240707523384196875, 5.000000000000000000 ) ) ;
#56442=ORIENTED_EDGE ( 'NONE', *, *, #57461, .T. ) ;
#56443=CARTESIAN_POINT ( 'NONE',  ( -12.79333936457838661, 21.75929247661549581, 4.998822639870701856 ) ) ;
#56444=PLANE ( 'NONE',  #96193 ) ;
#56447=CARTESIAN_POINT ( 'NONE',  ( 34.17183060077623225, -14.24070752338414003, 4.000000000000000000 ) ) ;
#56449=EDGE_LOOP ( 'NONE', ( #63178, #65971, #8571 ) ) ;
#56450=VERTEX_POINT ( 'NONE', #84124 ) ;
#56451=ORIENTED_EDGE ( 'NONE', *, *, #37987, .T. ) ;
#56453=VECTOR ( 'NONE', #56531, 1000.000000000000000 ) ;
#56454=ORIENTED_EDGE ( 'NONE', *, *, #79020, .T. ) ;
#56455=CARTESIAN_POINT ( 'NONE',  ( 3.183988606268992161, 28.73617430169789699, 5.000000000000000000 ) ) ;
#56456=CARTESIAN_POINT ( 'NONE',  ( 33.48921356237309510, -27.52281430457078670, 5.000000000000000000 ) ) ;
#56458=CARTESIAN_POINT ( 'NONE',  ( -69.48921356237309510, -27.52281430457103895, 5.000000000000000000 ) ) ;
#56459=DIRECTION ( 'NONE',  ( -0.000000000000000000, -0.3543493200069152693, 0.9351131265310292928 ) ) ;
#56460=ORIENTED_EDGE ( 'NONE', *, *, #122530, .F. ) ;
#56461=EDGE_CURVE ( 'NONE', #127371, #131836, #8948, .T. ) ;
#56462=DIRECTION ( 'NONE',  ( -0.7071067811865486830, -0.7071067811865464625, 0.000000000000000000 ) ) ;
#56463=DIRECTION ( 'NONE',  ( -0.7071067811865486830, -0.7071067811865464625, 0.000000000000000000 ) ) ;
#56466=ORIENTED_EDGE ( 'NONE', *, *, #131219, .T. ) ;
#56467=CARTESIAN_POINT ( 'NONE',  ( -48.18398860626899705, 28.73617430169820608, 5.000000000000000000 ) ) ;
#56469=ORIENTED_EDGE ( 'NONE', *, *, #75901, .T. ) ;
#56470=VERTEX_POINT ( 'NONE', #71098 ) ;
#56471=LINE ( 'NONE', #44126, #118624 ) ;
#56472=LINE ( 'NONE', #136112, #45519 ) ;
#56473=AXIS2_PLACEMENT_3D ( 'NONE', #66230, #49310, #11804 ) ;
#56474=LINE ( 'NONE', #79662, #39605 ) ;
#56476=LINE ( 'NONE', #102073, #120490 ) ;
#56477=EDGE_CURVE ( 'NONE', #25822, #33858, #61653, .T. ) ;
#56478=LINE ( 'NONE', #34686, #33548 ) ;
#56479=EDGE_CURVE ( 'NONE', #63415, #102811, #38345, .T. ) ;
#56480=VECTOR ( 'NONE', #25791, 999.9999999999998863 ) ;
#56482=ORIENTED_EDGE ( 'NONE', *, *, #98847, .F. ) ;
#56483=ADVANCED_FACE ( 'NONE', ( #39166 ), #26148, .F. ) ;
#56484=LINE ( 'NONE', #41999, #78122 ) ;
#56485=VERTEX_POINT ( 'NONE', #28292 ) ;
#56486=ORIENTED_EDGE ( 'NONE', *, *, #51351, .T. ) ;
#56488=EDGE_CURVE ( 'NONE', #42800, #46825, #137775, .T. ) ;
#56489=VECTOR ( 'NONE', #121704, 999.9999999999998863 ) ;
#56490=CARTESIAN_POINT ( 'NONE',  ( 7.499999999999947597, -20.53675388469229546, 2.352720554255910645 ) ) ;
#56491=ORIENTED_EDGE ( 'NONE', *, *, #96163, .T. ) ;
#56492=DIRECTION ( 'NONE',  ( -0.000000000000000000, -0.3543493200069152693, 0.9351131265310292928 ) ) ;
#56493=LINE ( 'NONE', #122387, #44901 ) ;
#56494=CARTESIAN_POINT ( 'NONE',  ( 0.000000000000000000, 0.000000000000000000, 5.000000000000000000 ) ) ;
#56495=CARTESIAN_POINT ( 'NONE',  ( -78.48921356237309510, -27.52281430457109934, 5.000000000000000000 ) ) ;
#56496=VERTEX_POINT ( 'NONE', #17396 ) ;
#56498=EDGE_CURVE ( 'NONE', #139011, #70912, #83387, .T. ) ;
#56499=EDGE_LOOP ( 'NONE', ( #123523, #25296, #124033, #20251 ) ) ;
#56500=LINE ( 'NONE', #91248, #34234 ) ;
#56503=ADVANCED_FACE ( 'NONE', ( #60966 ), #105126, .T. ) ;
#56504=EDGE_LOOP ( 'NONE', ( #39558, #119380, #21816, #21702, #97813 ) ) ;
#56505=DIRECTION ( 'NONE',  ( -0.7071067811865486830, -0.7071067811865464625, 0.000000000000000000 ) ) ;
#56506=ORIENTED_EDGE ( 'NONE', *, *, #94034, .T. ) ;
#56507=VERTEX_POINT ( 'NONE', #52860 ) ;
#56508=AXIS2_PLACEMENT_3D ( 'NONE', #60029, #104194, #88204 ) ;
#56509=ORIENTED_EDGE ( 'NONE', *, *, #10589, .F. ) ;
#56510=ADVANCED_FACE ( 'NONE', ( #97055 ), #141317, .F. ) ;
#56511=DIRECTION ( 'NONE',  ( -0.7071067811865486830, -0.7071067811865464625, 0.000000000000000000 ) ) ;
#56512=VECTOR ( 'NONE', #9412, 1000.000000000000000 ) ;
#56513=CARTESIAN_POINT ( 'NONE',  ( -16.49999999999988276, -20.94781430457062044, 5.000000000000000000 ) ) ;
#56514=FACE_OUTER_BOUND ( 'NONE', #51692, .T. ) ;
#56516=CARTESIAN_POINT ( 'NONE',  ( 17.99999999999986855, -18.03360074219755660, 5.000000000000000000 ) ) ;
#56517=PLANE ( 'NONE',  #73703 ) ;
#56518=EDGE_CURVE ( 'NONE', #133007, #40456, #86246, .T. ) ;
#56519=VECTOR ( 'NONE', #109613, 1000.000000000000000 ) ;
#56520=CARTESIAN_POINT ( 'NONE',  ( -34.49999999999975842, 12.05432934483081553, 4.994342998332167660 ) ) ;
#56522=VERTEX_POINT ( 'NONE', #120988 ) ;
#56523=CARTESIAN_POINT ( 'NONE',  ( -17.02886364525924989, -2.441401769420105339, 4.000000000000000000 ) ) ;
#56524=VECTOR ( 'NONE', #30477, 1000.000000000000000 ) ;
#56525=CARTESIAN_POINT ( 'NONE',  ( 33.79289321881321939, 9.759292476615623713, 5.000000000000000000 ) ) ;
#56526=DIRECTION ( 'NONE',  ( 0.7071067811865487940, -0.7071067811865463515, 0.000000000000000000 ) ) ;
#56527=ORIENTED_EDGE ( 'NONE', *, *, #98456, .T. ) ;
#56528=ORIENTED_EDGE ( 'NONE', *, *, #53594, .T. ) ;
#56529=EDGE_CURVE ( 'NONE', #104458, #101026, #65222, .T. ) ;
#56530=EDGE_LOOP ( 'NONE', ( #44117, #115723, #19699, #28791 ) ) ;
#56531=DIRECTION ( 'NONE',  ( 0.7071067811865487940, 0.7071067811865463515, -0.000000000000000000 ) ) ;
#56534=ORIENTED_EDGE ( 'NONE', *, *, #13430, .T. ) ;
#56536=VECTOR ( 'NONE', #78428, 1000.000000000000227 ) ;
#56537=FACE_OUTER_BOUND ( 'NONE', #86558, .T. ) ;
#56538=CARTESIAN_POINT ( 'NONE',  ( 12.18398860626900060, 28.73617430169795739, 5.000000000000000000 ) ) ;
#56540=VERTEX_POINT ( 'NONE', #84803 ) ;
#56541=DIRECTION ( 'NONE',  ( 0.7071067811865487940, 0.7071067811865463515, 0.000000000000000000 ) ) ;
#56542=ORIENTED_EDGE ( 'NONE', *, *, #104428, .T. ) ;
#56543=CARTESIAN_POINT ( 'NONE',  ( -9.511686059284260253, 6.759292476615653023, 16.35960578974471957 ) ) ;
#56545=ADVANCED_FACE ( 'NONE', ( #109406 ), #41285, .F. ) ;
#56546=VECTOR ( 'NONE', #80758, 1000.000000000000000 ) ;
#56550=( BOUNDED_CURVE ( )  B_SPLINE_CURVE ( 3, ( #123613, #101824, #35890, #13361 ),
 .UNSPECIFIED., .F., .F. ) 
 B_SPLINE_CURVE_WITH_KNOTS ( ( 4, 4 ),
 ( 5.043186909253412509, 5.074607125596358514 ),
 .UNSPECIFIED. ) 
 CURVE ( )  GEOMETRIC_REPRESENTATION_ITEM ( )  RATIONAL_B_SPLINE_CURVE ( ( 1.000000000000000000, 0.9999177325257868620, 0.9999177325257868620, 1.000000000000000000 ) ) 
 REPRESENTATION_ITEM ( '' )  );
#56551=DIRECTION ( 'NONE',  ( 0.6830127018922181881, 0.6830127018922202975, -0.2588190451025214056 ) ) ;
#56552=DIRECTION ( 'NONE',  ( 1.000000000000000000, 0.000000000000000000, 0.000000000000000000 ) ) ;
#56553=ORIENTED_EDGE ( 'NONE', *, *, #26593, .T. ) ;
#56554=CARTESIAN_POINT ( 'NONE',  ( -4.499999999999968914, -20.56887692260760048, 4.000000000000000000 ) ) ;
#56555=EDGE_LOOP ( 'NONE', ( #132459, #120635, #120437, #12017 ) ) ;
#56556=ORIENTED_EDGE ( 'NONE', *, *, #60727, .T. ) ;
#56557=FACE_OUTER_BOUND ( 'NONE', #131782, .T. ) ;
#56558=DIRECTION ( 'NONE',  ( 0.6830127018922180770, -0.6830127018922204085, -0.2588190451025214056 ) ) ;
#56559=AXIS2_PLACEMENT_3D ( 'NONE', #84548, #72277, #106243 ) ;
#56560=CARTESIAN_POINT ( 'NONE',  ( 27.70710678118635073, -3.740707523384246613, 5.000000000000000000 ) ) ;
#56561=DIRECTION ( 'NONE',  ( -0.7071067811865487940, 0.7071067811865463515, -0.000000000000000000 ) ) ;
#56562=CARTESIAN_POINT ( 'NONE',  ( -28.49999999999979750, 15.43112307739202471, 4.000000000000000000 ) ) ;
#56563=EDGE_LOOP ( 'NONE', ( #48451, #80001, #136142, #107427 ) ) ;
#56564=CARTESIAN_POINT ( 'NONE',  ( -60.29974487139158867, -27.71228299555248142, 4.000000000000000000 ) ) ;
#56565=DIRECTION ( 'NONE',  ( -0.000000000000000000, 0.000000000000000000, 1.000000000000000000 ) ) ;
#56566=LINE ( 'NONE', #88444, #37593 ) ;
#56567=EDGE_LOOP ( 'NONE', ( #137397, #91410, #118070, #60980 ) ) ;
#56568=CARTESIAN_POINT ( 'NONE',  ( 18.51665438641032324, 22.22500000000000142, 4.500000000000000888 ) ) ;
#56570=DIRECTION ( 'NONE',  ( -0.7071067811865487940, 0.7071067811865463515, -0.000000000000000000 ) ) ;
#56571=VERTEX_POINT ( 'NONE', #31158 ) ;
#56572=LINE ( 'NONE', #131954, #11612 ) ;
#56573=ORIENTED_EDGE ( 'NONE', *, *, #73192, .T. ) ;
#56574=ORIENTED_EDGE ( 'NONE', *, *, #14029, .F. ) ;
#56575=EDGE_CURVE ( 'NONE', #95760, #31203, #119537, .T. ) ;
#56576=LINE ( 'NONE', #12989, #121055 ) ;
#56578=FACE_OUTER_BOUND ( 'NONE', #33746, .T. ) ;
#56580=DIRECTION ( 'NONE',  ( 0.7071067811865486830, -0.7071067811865464625, -0.000000000000000000 ) ) ;
#56581=DIRECTION ( 'NONE',  ( -0.000000000000000000, 0.3543493200069153248, 0.9351131265310292928 ) ) ;
#56582=CARTESIAN_POINT ( 'NONE',  ( 21.32816939922338406, -21.74070752338405654, 4.000000000000000000 ) ) ;
#56584=LINE ( 'NONE', #100749, #143211 ) ;
#56585=DIRECTION ( 'NONE',  ( 0.7071067811865487940, 0.7071067811865463515, 0.000000000000000000 ) ) ;
#56587=EDGE_CURVE ( 'NONE', #123496, #57984, #43445, .T. ) ;
#56588=CARTESIAN_POINT ( 'NONE',  ( -8.395137668124739605, 21.75929247661549937, 21.32995629748188193 ) ) ;
#56589=CARTESIAN_POINT ( 'NONE',  ( 34.92499999999998295, -4.168643983631856287, 15.00153835162126903 ) ) ;
#56592=LINE ( 'NONE', #113769, #140813 ) ;
#56593=DIRECTION ( 'NONE',  ( 0.6830127018922180770, 0.6830127018922202975, -0.2588190451025213501 ) ) ;
#56594=LINE ( 'NONE', #110184, #82477 ) ;
#56595=ORIENTED_EDGE ( 'NONE', *, *, #115749, .T. ) ;
#56596=VECTOR ( 'NONE', #8100, 1000.000000000000227 ) ;
#56597=ORIENTED_EDGE ( 'NONE', *, *, #65968, .F. ) ;
#56600=ORIENTED_EDGE ( 'NONE', *, *, #138396, .T. ) ;
#56601=ORIENTED_EDGE ( 'NONE', *, *, #100448, .F. ) ;
#56602=CARTESIAN_POINT ( 'NONE',  ( 23.99999999999984013, -8.151047557385048492, -8.977947279169853800 ) ) ;
#56603=CARTESIAN_POINT ( 'NONE',  ( -33.18398860626899705, 28.73617430169810305, 5.000000000000000000 ) ) ;
#56604=CARTESIAN_POINT ( 'NONE',  ( -78.18398860626899705, 28.73617430169841924, 5.000000000000000000 ) ) ;
#56605=ORIENTED_EDGE ( 'NONE', *, *, #143458, .T. ) ;
#56606=CARTESIAN_POINT ( 'NONE',  ( -54.29974487139159578, -27.71228299555243879, 4.000000000000000000 ) ) ;
#56607=DIRECTION ( 'NONE',  ( -0.3543493200069162685, -0.000000000000000000, -0.9351131265310288487 ) ) ;
#56608=CARTESIAN_POINT ( 'NONE',  ( -17.01793588964200410, 8.788317580041923094, 4.329525704382049867 ) ) ;
#56609=LINE ( 'NONE', #45713, #39691 ) ;
#56610=EDGE_CURVE ( 'NONE', #125114, #71992, #131062, .T. ) ;
#56611=ORIENTED_EDGE ( 'NONE', *, *, #80232, .T. ) ;
#56612=FACE_OUTER_BOUND ( 'NONE', #36280, .T. ) ;
#56613=EDGE_CURVE ( 'NONE', #8014, #45414, #53618, .T. ) ;
#56615=LINE ( 'NONE', #3570, #60639 ) ;
#56616=VECTOR ( 'NONE', #6842, 999.9999999999998863 ) ;
#56617=DIRECTION ( 'NONE',  ( -0.7071067811865486830, -0.7071067811865464625, 0.000000000000000000 ) ) ;
#56618=CARTESIAN_POINT ( 'NONE',  ( -23.99999999999982592, -1.447814304570811617, 5.000000000000000000 ) ) ;
#56619=CARTESIAN_POINT ( 'NONE',  ( 3.489213562373097322, -27.52281430457057709, 5.000000000000000000 ) ) ;
#56621=DIRECTION ( 'NONE',  ( -0.7071067811865487940, 0.7071067811865463515, 0.000000000000000000 ) ) ;
#56622=AXIS2_PLACEMENT_3D ( 'NONE', #76346, #29254, #86518 ) ;
#56623=EDGE_LOOP ( 'NONE', ( #114016, #27530, #44940, #142470 ) ) ;
#56624=EDGE_LOOP ( 'NONE', ( #86155, #62027, #25125, #44693 ) ) ;
#56626=EDGE_LOOP ( 'NONE', ( #80649, #29983, #48966, #9373 ) ) ;
#56627=ADVANCED_FACE ( 'NONE', ( #64480 ), #131885, .F. ) ;
#56628=VECTOR ( 'NONE', #13534, 999.9999999999998863 ) ;
#56629=CARTESIAN_POINT ( 'NONE',  ( 34.42499999999998295, -21.72500000000000142, 0.5000000000000000000 ) ) ;
#56630=FACE_OUTER_BOUND ( 'NONE', #49825, .T. ) ;
#56631=EDGE_CURVE ( 'NONE', #3592, #136288, #142067, .T. ) ;
#56632=LINE ( 'NONE', #33438, #46736 ) ;
#56633=CARTESIAN_POINT ( 'NONE',  ( 30.48921356237309510, -27.52281430457076894, 5.000000000000000000 ) ) ;
#56635=VECTOR ( 'NONE', #38325, 1000.000000000000000 ) ;
#56636=VERTEX_POINT ( 'NONE', #118107 ) ;
#56638=EDGE_CURVE ( 'NONE', #112641, #127735, #107256, .T. ) ;
#56639=CARTESIAN_POINT ( 'NONE',  ( 8.816011393731004731, 28.73617430169781173, 5.000000000000000000 ) ) ;
#56640=ORIENTED_EDGE ( 'NONE', *, *, #80794, .F. ) ;
#56641=EDGE_LOOP ( 'NONE', ( #95347, #120362, #22669, #107604 ) ) ;
#56643=VERTEX_POINT ( 'NONE', #20958 ) ;
#56644=DIRECTION ( 'NONE',  ( -0.000000000000000000, 0.3543493200069153248, 0.9351131265310292928 ) ) ;
#56648=VECTOR ( 'NONE', #56561, 999.9999999999998863 ) ;
#56652=CARTESIAN_POINT ( 'NONE',  ( -29.20710678118634007, -5.240707523384228850, 5.000000000000000000 ) ) ;
#56653=ORIENTED_EDGE ( 'NONE', *, *, #64600, .F. ) ;
#56654=ORIENTED_EDGE ( 'NONE', *, *, #90137, .F. ) ;
#56655=VERTEX_POINT ( 'NONE', #56513 ) ;
#56657=EDGE_CURVE ( 'NONE', #78474, #118381, #57207, .T. ) ;
#56658=FACE_OUTER_BOUND ( 'NONE', #9158, .T. ) ;
#56659=DIRECTION ( 'NONE',  ( 0.7071067811865487940, 0.7071067811865463515, -0.000000000000000000 ) ) ;
#56660=ORIENTED_EDGE ( 'NONE', *, *, #115661, .F. ) ;
#56661=CARTESIAN_POINT ( 'NONE',  ( -11.99999999999991296, -2.904428200921318481, -6.989807076074915138 ) ) ;
#56663=CARTESIAN_POINT ( 'NONE',  ( -5.510786437626906675, -27.52281430457051314, 5.000000000000000000 ) ) ;
#56665=CARTESIAN_POINT ( 'NONE',  ( 1.176659101599728752, 5.259292476615672562, 15.86257073897097847 ) ) ;
#56666=FACE_BOUND ( 'NONE', #41618, .T. ) ;
#56667=EDGE_CURVE ( 'NONE', #35104, #59514, #102118, .T. ) ;
#56668=ORIENTED_EDGE ( 'NONE', *, *, #91337, .F. ) ;
#56669=CARTESIAN_POINT ( 'NONE',  ( 27.48921356237309155, -27.52281430457074762, 5.000000000000000000 ) ) ;
#56670=CARTESIAN_POINT ( 'NONE',  ( 23.20710678118638626, -2.240707523384260824, 5.000000000000000000 ) ) ;
#56674=ORIENTED_EDGE ( 'NONE', *, *, #9114, .F. ) ;
#56677=VERTEX_POINT ( 'NONE', #132631 ) ;
#56678=ORIENTED_EDGE ( 'NONE', *, *, #36890, .T. ) ;
#56681=ORIENTED_EDGE ( 'NONE', *, *, #104845, .T. ) ;
#56683=CARTESIAN_POINT ( 'NONE',  ( 5.207106781186502609, -20.24070752338407431, 5.000000000000000000 ) ) ;
#56684=CARTESIAN_POINT ( 'NONE',  ( -69.29974487139159578, -27.71228299555254537, 4.000000000000000000 ) ) ;
#56686=CARTESIAN_POINT ( 'NONE',  ( 0.4116149059483135697, 22.22500000000000142, 4.777194822843816802 ) ) ;
#56689=VECTOR ( 'NONE', #84127, 1000.000000000000000 ) ;
#56692=DIRECTION ( 'NONE',  ( -0.7071067811865486830, 0.7071067811865464625, 0.000000000000000000 ) ) ;
#56693=VERTEX_POINT ( 'NONE', #112282 ) ;
#56694=ORIENTED_EDGE ( 'NONE', *, *, #65779, .F. ) ;
#56695=ORIENTED_EDGE ( 'NONE', *, *, #134300, .F. ) ;
#56696=ORIENTED_EDGE ( 'NONE', *, *, #121246, .F. ) ;
#56697=DIRECTION ( 'NONE',  ( -0.7071067811865487940, 0.7071067811865463515, -0.000000000000000000 ) ) ;
#56699=VERTEX_POINT ( 'NONE', #68099 ) ;
#56700=ORIENTED_EDGE ( 'NONE', *, *, #31991, .T. ) ;
#56701=DIRECTION ( 'NONE',  ( -0.3543493200069162685, -0.000000000000000000, -0.9351131265310288487 ) ) ;
#56702=DIRECTION ( 'NONE',  ( -0.000000000000000000, 0.000000000000000000, 1.000000000000000000 ) ) ;
#56703=VERTEX_POINT ( 'NONE', #79696 ) ;
#56704=EDGE_CURVE ( 'NONE', #106514, #61464, #78227, .T. ) ;
#56705=CARTESIAN_POINT ( 'NONE',  ( -8.999999999999936051, 13.55218569542903495, 5.000000000000000000 ) ) ;
#56706=EDGE_CURVE ( 'NONE', #37184, #123300, #89789, .T. ) ;
#56707=LINE ( 'NONE', #100869, #86145 ) ;
#56708=EDGE_CURVE ( 'NONE', #61158, #15400, #67354, .T. ) ;
#56709=VECTOR ( 'NONE', #107364, 1000.000000000000000 ) ;
#56711=FACE_OUTER_BOUND ( 'NONE', #94703, .T. ) ;
#56712=ORIENTED_EDGE ( 'NONE', *, *, #40867, .T. ) ;
#56714=CARTESIAN_POINT ( 'NONE',  ( -10.49999999999992895, 0.4311230773921849169, 4.000000000000000000 ) ) ;
#56715=VECTOR ( 'NONE', #72102, 1000.000000000000000 ) ;
#56716=DIRECTION ( 'NONE',  ( 0.7071067811865487940, 0.7071067811865463515, 0.000000000000000000 ) ) ;
#56717=LINE ( 'NONE', #79895, #74362 ) ;
#56718=LINE ( 'NONE', #67576, #75040 ) ;
#56719=DIRECTION ( 'NONE',  ( -0.000000000000000000, 0.3543493200069153248, 0.9351131265310292928 ) ) ;
#56720=VERTEX_POINT ( 'NONE', #134031 ) ;
#56721=PLANE ( 'NONE',  #134183 ) ;
#56722=ORIENTED_EDGE ( 'NONE', *, *, #30537, .F. ) ;
#56723=PLANE ( 'NONE',  #12701 ) ;
#56724=EDGE_CURVE ( 'NONE', #66617, #118405, #35999, .T. ) ;
#56725=CARTESIAN_POINT ( 'NONE',  ( 21.32816939922338051, 14.25929247661557397, 4.000000000000000000 ) ) ;
#56728=FACE_OUTER_BOUND ( 'NONE', #75390, .T. ) ;
#56729=VECTOR ( 'NONE', #59917, 1000.000000000000000 ) ;
#56730=DIRECTION ( 'NONE',  ( 0.6830127018922181881, 0.6830127018922202975, -0.2588190451025214056 ) ) ;
#56732=VERTEX_POINT ( 'NONE', #125857 ) ;
#56733=PLANE ( 'NONE',  #21470 ) ;
#56734=ORIENTED_EDGE ( 'NONE', *, *, #115787, .F. ) ;
#56736=CARTESIAN_POINT ( 'NONE',  ( 6.938893903907228378E-15, 11.96639925780214675, 5.000000000000000000 ) ) ;
#56737=ORIENTED_EDGE ( 'NONE', *, *, #77218, .F. ) ;
#56738=EDGE_LOOP ( 'NONE', ( #73631, #20204, #35440 ) ) ;
#56739=CARTESIAN_POINT ( 'NONE',  ( -34.92500000000001137, -22.22500000000000142, 4.000000000000000000 ) ) ;
#56740=DIRECTION ( 'NONE',  ( 0.7071067811865486830, -0.7071067811865464625, -0.000000000000000000 ) ) ;
#56742=VECTOR ( 'NONE', #20338, 1000.000000000000000 ) ;
#56745=VECTOR ( 'NONE', #75914, 999.9999999999998863 ) ;
#56747=DIRECTION ( 'NONE',  ( 0.6830127018922181881, 0.6830127018922202975, -0.2588190451025214056 ) ) ;
#56748=ORIENTED_EDGE ( 'NONE', *, *, #6116, .T. ) ;
#56750=CARTESIAN_POINT ( 'NONE',  ( 9.005480084712511157, 28.92564299267931816, 4.000000000000000000 ) ) ;
#56751=CARTESIAN_POINT ( 'NONE',  ( -34.92500000000001137, 21.72500000000000142, 5.000000000000000000 ) ) ;
#56753=DIRECTION ( 'NONE',  ( -0.000000000000000000, 0.000000000000000000, 1.000000000000000000 ) ) ;
#56754=DIRECTION ( 'NONE',  ( -0.000000000000000000, -0.3543493200069152693, 0.9351131265310292928 ) ) ;
#56756=LINE ( 'NONE', #120489, #69777 ) ;
#56757=EDGE_LOOP ( 'NONE', ( #105004, #85509, #232, #114597 ) ) ;
#56759=ORIENTED_EDGE ( 'NONE', *, *, #22708, .T. ) ;
#56760=LINE ( 'NONE', #22613, #111331 ) ;
#56761=VERTEX_POINT ( 'NONE', #67940 ) ;
#56763=ORIENTED_EDGE ( 'NONE', *, *, #124211, .F. ) ;
#56765=DIRECTION ( 'NONE',  ( -0.7071067811865486830, -0.7071067811865464625, -0.000000000000000000 ) ) ;
#56766=VERTEX_POINT ( 'NONE', #104051 ) ;
#56767=CARTESIAN_POINT ( 'NONE',  ( 13.49999999999991118, -7.420205493532887608, -2.617629953481223293 ) ) ;
#56768=DIRECTION ( 'NONE',  ( 0.7071067811865487940, 0.7071067811865463515, 0.000000000000000000 ) ) ;
#56769=ADVANCED_FACE ( 'NONE', ( #26530 ), #14920, .F. ) ;
#56770=LINE ( 'NONE', #142323, #23160 ) ;
#56771=CARTESIAN_POINT ( 'NONE',  ( -6.792893218813407685, 3.759292476615680112, 5.000000000000000000 ) ) ;
#56773=EDGE_CURVE ( 'NONE', #82756, #23807, #13470, .T. ) ;
#56774=ORIENTED_EDGE ( 'NONE', *, *, #114687, .T. ) ;
#56775=LINE ( 'NONE', #26249, #39537 ) ;
#56776=LINE ( 'NONE', #98096, #93182 ) ;
#56780=CARTESIAN_POINT ( 'NONE',  ( 9.654944837453772521, 5.259292476615669010, 12.77922209995895919 ) ) ;
#56781=LINE ( 'NONE', #137159, #50468 ) ;
#56782=EDGE_CURVE ( 'NONE', #18270, #98423, #80225, .T. ) ;
#56784=EDGE_CURVE ( 'NONE', #5826, #100179, #124409, .T. ) ;
#56785=DIRECTION ( 'NONE',  ( 0.7071067811865486830, -0.7071067811865464625, -0.000000000000000000 ) ) ;
#56786=DIRECTION ( 'NONE',  ( -0.000000000000000000, 0.000000000000000000, 1.000000000000000000 ) ) ;
#56787=ORIENTED_EDGE ( 'NONE', *, *, #101420, .F. ) ;
#56788=VERTEX_POINT ( 'NONE', #112813 ) ;
#56790=EDGE_CURVE ( 'NONE', #82218, #108587, #80920, .T. ) ;
#56791=DIRECTION ( 'NONE',  ( -0.6830127018922181881, 0.6830127018922202975, -0.2588190451025214056 ) ) ;
#56792=VERTEX_POINT ( 'NONE', #135997 ) ;
#56793=LINE ( 'NONE', #56067, #133597 ) ;
#56794=DIRECTION ( 'NONE',  ( -0.7071067811865487940, 0.7071067811865463515, 0.000000000000000000 ) ) ;
#56795=EDGE_CURVE ( 'NONE', #72734, #106882, #101943, .T. ) ;
#56797=VERTEX_POINT ( 'NONE', #3997 ) ;
#56799=ORIENTED_EDGE ( 'NONE', *, *, #7544, .F. ) ;
#56800=DIRECTION ( 'NONE',  ( 0.000000000000000000, 0.000000000000000000, 1.000000000000000000 ) ) ;
#56801=EDGE_CURVE ( 'NONE', #42167, #89926, #136702, .T. ) ;
#56802=FACE_OUTER_BOUND ( 'NONE', #102683, .T. ) ;
#56803=DIRECTION ( 'NONE',  ( -0.7071067811865486830, -0.7071067811865464625, 0.000000000000000000 ) ) ;
#56805=VERTEX_POINT ( 'NONE', #69331 ) ;
#56806=FACE_OUTER_BOUND ( 'NONE', #4897, .T. ) ;
#56807=VERTEX_POINT ( 'NONE', #125116 ) ;
#56808=LINE ( 'NONE', #100971, #70260 ) ;
#56810=CARTESIAN_POINT ( 'NONE',  ( -25.49999999999982236, 9.052185695429074030, 5.000000000000000000 ) ) ;
#56811=EDGE_CURVE ( 'NONE', #131612, #62746, #58501, .T. ) ;
#56812=DIRECTION ( 'NONE',  ( 0.7071067811865487940, -0.7071067811865463515, 0.000000000000000000 ) ) ;
#56813=CARTESIAN_POINT ( 'NONE',  ( -14.28242261357422116, -21.73023691814492864, 5.000000000000000888 ) ) ;
#56814=VECTOR ( 'NONE', #33253, 1000.000000000000000 ) ;
#56815=ORIENTED_EDGE ( 'NONE', *, *, #132405, .F. ) ;
#56816=DIRECTION ( 'NONE',  ( -0.000000000000000000, 0.000000000000000000, 1.000000000000000000 ) ) ;
#56820=EDGE_CURVE ( 'NONE', #34380, #6222, #89636, .T. ) ;
#56821=CARTESIAN_POINT ( 'NONE',  ( -14.70025512860841133, -27.71228299555195917, 4.000000000000000000 ) ) ;
#56822=CARTESIAN_POINT ( 'NONE',  ( -45.18398860626900415, 28.73617430169818832, 5.000000000000000000 ) ) ;
#56825=ORIENTED_EDGE ( 'NONE', *, *, #49894, .F. ) ;
#56826=( BOUNDED_CURVE ( )  B_SPLINE_CURVE ( 3, ( #74964, #19821, #61258, #64062 ),
 .UNSPECIFIED., .F., .F. ) 
 B_SPLINE_CURVE_WITH_KNOTS ( ( 4, 4 ),
 ( 4.350170835173025274, 4.500739107949270235 ),
 .UNSPECIFIED. ) 
 CURVE ( )  GEOMETRIC_REPRESENTATION_ITEM ( )  RATIONAL_B_SPLINE_CURVE ( ( 1.000000000000000000, 0.9981116584018941973, 0.9981116584018941973, 1.000000000000000000 ) ) 
 REPRESENTATION_ITEM ( '' )  );
#56827=ADVANCED_FACE ( 'NONE', ( #25075 ), #1860, .F. ) ;
#56828=AXIS2_PLACEMENT_3D ( 'NONE', #64545, #36215, #135529 ) ;
#56829=LINE ( 'NONE', #111132, #93115 ) ;
#56830=VERTEX_POINT ( 'NONE', #113516 ) ;
#56832=DIRECTION ( 'NONE',  ( 1.000000000000000000, 0.000000000000000000, 0.000000000000000000 ) ) ;
#56833=CARTESIAN_POINT ( 'NONE',  ( -27.18398860626900060, 28.73617430169806042, 5.000000000000000000 ) ) ;
#56834=LINE ( 'NONE', #100994, #69411 ) ;
#56835=EDGE_CURVE ( 'NONE', #28781, #58036, #57049, .T. ) ;
#56836=PLANE ( 'NONE',  #115951 ) ;
#56837=FACE_BOUND ( 'NONE', #142518, .T. ) ;
#56838=DIRECTION ( 'NONE',  ( 1.000000000000000000, 0.000000000000000000, 0.000000000000000000 ) ) ;
#56839=PLANE ( 'NONE',  #58368 ) ;
#56840=CARTESIAN_POINT ( 'NONE',  ( 28.49999999999980105, -8.568876922607731927, 4.000000000000000000 ) ) ;
#56841=CARTESIAN_POINT ( 'NONE',  ( 9.183988606268997046, 28.73617430169793607, 5.000000000000000000 ) ) ;
#56844=VECTOR ( 'NONE', #99891, 1000.000000000000000 ) ;
#56845=VERTEX_POINT ( 'NONE', #14209 ) ;
#56846=VECTOR ( 'NONE', #67756, 999.9999999999998863 ) ;
#56847=VECTOR ( 'NONE', #69615, 1000.000000000000000 ) ;
#56848=ORIENTED_EDGE ( 'NONE', *, *, #36437, .F. ) ;
#56850=ORIENTED_EDGE ( 'NONE', *, *, #73955, .T. ) ;
#56851=CARTESIAN_POINT ( 'NONE',  ( -26.99999999999981171, -21.84840872380826937, 2.849755605029545169 ) ) ;
#56852=VECTOR ( 'NONE', #66288, 1000.000000000000000 ) ;
#56853=EDGE_CURVE ( 'NONE', #112333, #122403, #46171, .T. ) ;
#56854=LINE ( 'NONE', #40084, #34873 ) ;
#56856=DIRECTION ( 'NONE',  ( 1.000000000000000000, 0.000000000000000000, 0.000000000000000000 ) ) ;
#56857=EDGE_CURVE ( 'NONE', #30899, #103815, #123724, .T. ) ;
#56859=DIRECTION ( 'NONE',  ( 0.6830127018922181881, 0.6830127018922202975, -0.2588190451025214056 ) ) ;
#56861=DIRECTION ( 'NONE',  ( -0.6830127018922181881, 0.6830127018922202975, -0.2588190451025214056 ) ) ;
#56862=LINE ( 'NONE', #132981, #72808 ) ;
#56864=LINE ( 'NONE', #101020, #104131 ) ;
#56865=VERTEX_POINT ( 'NONE', #3319 ) ;
#56866=VERTEX_POINT ( 'NONE', #36673 ) ;
#56867=LINE ( 'NONE', #103172, #58994 ) ;
#56868=CARTESIAN_POINT ( 'NONE',  ( 10.93003974513585064, -0.7407075233842805861, 13.87443053587608333 ) ) ;
#56869=ORIENTED_EDGE ( 'NONE', *, *, #120630, .F. ) ;
#56873=ORIENTED_EDGE ( 'NONE', *, *, #48196, .T. ) ;
#56874=DIRECTION ( 'NONE',  ( -0.7071067811865486830, -0.7071067811865464625, 0.000000000000000000 ) ) ;
#56875=EDGE_CURVE ( 'NONE', #18494, #132815, #5455, .T. ) ;
#56879=VERTEX_POINT ( 'NONE', #94616 ) ;
#56880=CARTESIAN_POINT ( 'NONE',  ( -34.92500000000001137, -13.27521306008089930, -8.452357796116194422 ) ) ;
#56881=CARTESIAN_POINT ( 'NONE',  ( -11.20666063542143753, 21.75929247661549937, 4.998822639870708073 ) ) ;
#56882=DIRECTION ( 'NONE',  ( 0.7071067811865487940, 0.7071067811865463515, 0.000000000000000000 ) ) ;
#56883=DIRECTION ( 'NONE',  ( -0.7071067811865487940, 0.7071067811865463515, -0.000000000000000000 ) ) ;
#56884=ORIENTED_EDGE ( 'NONE', *, *, #134231, .F. ) ;
#56885=ORIENTED_EDGE ( 'NONE', *, *, #19235, .F. ) ;
#56886=LINE ( 'NONE', #67764, #100118 ) ;
#56888=ORIENTED_EDGE ( 'NONE', *, *, #57926, .F. ) ;
#56890=LINE ( 'NONE', #35854, #14707 ) ;
#56891=FACE_OUTER_BOUND ( 'NONE', #138771, .T. ) ;
#56892=CARTESIAN_POINT ( 'NONE',  ( 27.18398860626900060, 28.73617430169806042, 5.000000000000000000 ) ) ;
#56893=CARTESIAN_POINT ( 'NONE',  ( -4.499999999999976019, 16.18958161055402201, -11.56426086740812487 ) ) ;
#56894=CARTESIAN_POINT ( 'NONE',  ( 18.18398860626898994, 28.73617430169800002, 5.000000000000000000 ) ) ;
#56895=LINE ( 'NONE', #24238, #23988 ) ;
#56896=CARTESIAN_POINT ( 'NONE',  ( -29.99451991528749417, 28.92564299267958816, 4.000000000000000000 ) ) ;
#56897=EDGE_LOOP ( 'NONE', ( #59564, #18304, #117624, #83203 ) ) ;
#56898=ORIENTED_EDGE ( 'NONE', *, *, #89851, .F. ) ;
#56899=FACE_OUTER_BOUND ( 'NONE', #116604, .T. ) ;
#56900=DIRECTION ( 'NONE',  ( -0.7071067811865487940, 0.7071067811865463515, -0.000000000000000000 ) ) ;
#56902=DIRECTION ( 'NONE',  ( 1.000000000000000000, 0.000000000000000000, 0.000000000000000000 ) ) ;
#56903=ORIENTED_EDGE ( 'NONE', *, *, #127783, .T. ) ;
#56904=CARTESIAN_POINT ( 'NONE',  ( 7.171830600776423204, 15.75929247661555976, 4.000000000000000000 ) ) ;
#56905=DIRECTION ( 'NONE',  ( -0.000000000000000000, 0.3543493200069153248, 0.9351131265310292928 ) ) ;
#56906=CARTESIAN_POINT ( 'NONE',  ( 13.11345250541376473, 3.796869306786346598, 4.054893674211259125 ) ) ;
#56907=VECTOR ( 'NONE', #43229, 999.9999999999998863 ) ;
#56908=ORIENTED_EDGE ( 'NONE', *, *, #12582, .F. ) ;
#56911=CARTESIAN_POINT ( 'NONE',  ( 17.51078643762690845, -27.52281430457043143, 5.000000000000000000 ) ) ;
#56913=DIRECTION ( 'NONE',  ( -0.7071067811865486830, 0.7071067811865464625, 0.000000000000000000 ) ) ;
#56914=VECTOR ( 'NONE', #128745, 1000.000000000000000 ) ;
#56915=FACE_OUTER_BOUND ( 'NONE', #7058, .T. ) ;
#56916=LINE ( 'NONE', #35881, #18635 ) ;
#56917=ORIENTED_EDGE ( 'NONE', *, *, #93252, .F. ) ;
#56918=CARTESIAN_POINT ( 'NONE',  ( -3.328169399223496860, -9.740707523384180888, 4.000000000000000000 ) ) ;
#56919=ORIENTED_EDGE ( 'NONE', *, *, #139290, .F. ) ;
#56922=DIRECTION ( 'NONE',  ( -0.6830127018922181881, 0.6830127018922202975, -0.2588190451025214056 ) ) ;
#56923=DIRECTION ( 'NONE',  ( 0.3543493200069162685, -0.000000000000000000, -0.9351131265310288487 ) ) ;
#56924=CARTESIAN_POINT ( 'NONE',  ( -0.4892135623730947680, -27.52281430457055578, 5.000000000000000000 ) ) ;
#56925=DIRECTION ( 'NONE',  ( -0.6830127018922180770, -0.6830127018922204085, -0.2588190451025213501 ) ) ;
#56926=EDGE_CURVE ( 'NONE', #6521, #78331, #6155, .T. ) ;
#56927=EDGE_CURVE ( 'NONE', #27120, #1016, #20441, .T. ) ;
#56929=ORIENTED_EDGE ( 'NONE', *, *, #28532, .T. ) ;
#56930=CARTESIAN_POINT ( 'NONE',  ( 5.816011393731002066, 28.73617430169783304, 5.000000000000000000 ) ) ;
#56932=CARTESIAN_POINT ( 'NONE',  ( -8.510786437626906675, -27.52281430457049183, 5.000000000000000000 ) ) ;
#56933=VECTOR ( 'NONE', #13397, 1000.000000000000227 ) ;
#56934=DIRECTION ( 'NONE',  ( 0.7071067811865487940, 0.7071067811865463515, 0.000000000000000000 ) ) ;
#56939=VECTOR ( 'NONE', #43734, 1000.000000000000000 ) ;
#56940=LINE ( 'NONE', #102573, #106229 ) ;
#56941=ORIENTED_EDGE ( 'NONE', *, *, #92410, .T. ) ;
#56943=CARTESIAN_POINT ( 'NONE',  ( 8.241399257801971245, 21.72500000000000142, 5.000000000000000000 ) ) ;
#56944=EDGE_CURVE ( 'NONE', #128780, #12755, #131372, .T. ) ;
#56945=PLANE ( 'NONE',  #6885 ) ;
#56946=DIRECTION ( 'NONE',  ( 0.7071067811865487940, 0.7071067811865463515, -0.000000000000000000 ) ) ;
#56947=VECTOR ( 'NONE', #87386, 1000.000000000000227 ) ;
#56948=ADVANCED_FACE ( 'NONE', ( #93913 ), #116390, .F. ) ;
#56952=CARTESIAN_POINT ( 'NONE',  ( 0.000000000000000000, 0.000000000000000000, 5.000000000000000000 ) ) ;
#56954=ORIENTED_EDGE ( 'NONE', *, *, #128292, .F. ) ;
#56955=VERTEX_POINT ( 'NONE', #17082 ) ;
#56956=CARTESIAN_POINT ( 'NONE',  ( 32.99999999999977263, -10.06887692260770528, 4.000000000000000000 ) ) ;
#56957=EDGE_CURVE ( 'NONE', #13150, #20021, #106191, .T. ) ;
#56958=LINE ( 'NONE', #43920, #99929 ) ;
#56959=CARTESIAN_POINT ( 'NONE',  ( -17.81601139373099940, 28.73617430169775133, 5.000000000000000000 ) ) ;
#56960=PLANE ( 'NONE',  #120610 ) ;
#56961=LINE ( 'NONE', #37328, #121629 ) ;
#56962=ORIENTED_EDGE ( 'NONE', *, *, #93656, .F. ) ;
#56964=FACE_OUTER_BOUND ( 'NONE', #105667, .T. ) ;
#56965=FACE_OUTER_BOUND ( 'NONE', #79845, .T. ) ;
#56966=LINE ( 'NONE', #99713, #130429 ) ;
#56967=EDGE_CURVE ( 'NONE', #51992, #111906, #39567, .T. ) ;
#56968=CARTESIAN_POINT ( 'NONE',  ( -5.510786437626906675, -27.52281430457051314, 5.000000000000000000 ) ) ;
#56969=EDGE_LOOP ( 'NONE', ( #11653, #108932, #33669, #61847 ) ) ;
#56970=ORIENTED_EDGE ( 'NONE', *, *, #96054, .F. ) ;
#56972=ORIENTED_EDGE ( 'NONE', *, *, #23651, .F. ) ;
#56973=DIRECTION ( 'NONE',  ( -0.7071067811865486830, -0.7071067811865464625, 0.000000000000000000 ) ) ;
#56975=DIRECTION ( 'NONE',  ( -0.7071067811865486830, -0.7071067811865464625, -0.000000000000000000 ) ) ;
#56977=FACE_OUTER_BOUND ( 'NONE', #6995, .T. ) ;
#56978=DIRECTION ( 'NONE',  ( -0.7071067811865487940, 0.7071067811865463515, -0.000000000000000000 ) ) ;
#56980=VERTEX_POINT ( 'NONE', #83051 ) ;
#56981=PLANE ( 'NONE',  #63160 ) ;
#56983=EDGE_CURVE ( 'NONE', #141725, #68424, #127252, .T. ) ;
#56984=EDGE_LOOP ( 'NONE', ( #119554, #109748, #106992, #78803 ) ) ;
#56985=CARTESIAN_POINT ( 'NONE',  ( -21.41161490594815575, 22.22500000000000142, 4.777194822843816802 ) ) ;
#56987=DIRECTION ( 'NONE',  ( -0.7071067811865487940, 0.7071067811865463515, -0.000000000000000000 ) ) ;
#56988=CARTESIAN_POINT ( 'NONE',  ( 14.54487008052911534, -0.7407075233842805861, 4.335043535661647240 ) ) ;
#56990=VERTEX_POINT ( 'NONE', #64693 ) ;
#56991=EDGE_CURVE ( 'NONE', #8350, #140410, #104795, .T. ) ;
#56992=FACE_BOUND ( 'NONE', #115027, .T. ) ;
#56993=DIRECTION ( 'NONE',  ( 0.3543493200069162685, -0.000000000000000000, -0.9351131265310288487 ) ) ;
#56994=CARTESIAN_POINT ( 'NONE',  ( 8.999999999999941380, 16.55218569542900298, 5.000000000000000000 ) ) ;
#56997=( BOUNDED_CURVE ( )  B_SPLINE_CURVE ( 3, ( #51382, #6377, #62260, #94143 ),
 .UNSPECIFIED., .F., .T. ) 
 B_SPLINE_CURVE_WITH_KNOTS ( ( 4, 4 ),
 ( 1.208578181583236821, 1.359146454359418277 ),
 .UNSPECIFIED. ) 
 CURVE ( )  GEOMETRIC_REPRESENTATION_ITEM ( )  RATIONAL_B_SPLINE_CURVE ( ( 1.000000000000000000, 0.9981116584018958626, 0.9981116584018958626, 1.000000000000000000 ) ) 
 REPRESENTATION_ITEM ( '' )  );
#56998=PLANE ( 'NONE',  #92928 ) ;
#57000=VECTOR ( 'NONE', #66451, 999.9999999999998863 ) ;
#57001=ORIENTED_EDGE ( 'NONE', *, *, #122970, .T. ) ;
#57002=ORIENTED_EDGE ( 'NONE', *, *, #5869, .F. ) ;
#57004=ORIENTED_EDGE ( 'NONE', *, *, #45995, .T. ) ;
#57006=EDGE_CURVE ( 'NONE', #129739, #8240, #9557, .T. ) ;
#57007=CARTESIAN_POINT ( 'NONE',  ( 33.48921356237309510, -27.52281430457078670, 5.000000000000000000 ) ) ;
#57008=EDGE_LOOP ( 'NONE', ( #86960, #106283, #137383, #80834 ) ) ;
#57009=DIRECTION ( 'NONE',  ( 0.6830127018922181881, 0.6830127018922202975, -0.2588190451025214056 ) ) ;
#57010=LINE ( 'NONE', #47575, #89472 ) ;
#57012=ORIENTED_EDGE ( 'NONE', *, *, #140237, .T. ) ;
#57014=PLANE ( 'NONE',  #102809 ) ;
#57015=EDGE_CURVE ( 'NONE', #81561, #28403, #65429, .T. ) ;
#57016=LINE ( 'NONE', #111345, #64011 ) ;
#57017=VECTOR ( 'NONE', #95937, 999.9999999999998863 ) ;
#57020=DIRECTION ( 'NONE',  ( -0.000000000000000000, -0.3543493200069152693, 0.9351131265310292928 ) ) ;
#57021=CARTESIAN_POINT ( 'NONE',  ( -42.48921356237308800, -27.52281430457085065, 5.000000000000000000 ) ) ;
#57023=ORIENTED_EDGE ( 'NONE', *, *, #107276, .F. ) ;
#57025=DIRECTION ( 'NONE',  ( 0.7071067811865487940, 0.7071067811865463515, 0.000000000000000000 ) ) ;
#57027=ADVANCED_FACE ( 'NONE', ( #49008 ), #111012, .T. ) ;
#57028=VECTOR ( 'NONE', #142700, 1000.000000000000000 ) ;
#57029=ORIENTED_EDGE ( 'NONE', *, *, #26656, .T. ) ;
#57032=ORIENTED_EDGE ( 'NONE', *, *, #75403, .F. ) ;
#57033=VECTOR ( 'NONE', #48200, 1000.000000000000227 ) ;
#57034=PLANE ( 'NONE',  #83740 ) ;
#57035=VECTOR ( 'NONE', #121118, 1000.000000000000227 ) ;
#57038=LINE ( 'NONE', #124400, #40513 ) ;
#57040=VECTOR ( 'NONE', #105740, 1000.000000000000227 ) ;
#57041=LINE ( 'NONE', #99053, #133624 ) ;
#57042=VERTEX_POINT ( 'NONE', #10976 ) ;
#57043=PLANE ( 'NONE',  #141303 ) ;
#57044=VECTOR ( 'NONE', #102378, 999.9999999999998863 ) ;
#57045=LINE ( 'NONE', #136697, #21604 ) ;
#57046=ORIENTED_EDGE ( 'NONE', *, *, #50073, .F. ) ;
#57047=EDGE_CURVE ( 'NONE', #105802, #134641, #44392, .T. ) ;
#57048=DIRECTION ( 'NONE',  ( -0.7071067811865487940, 0.7071067811865463515, -0.000000000000000000 ) ) ;
#57049=LINE ( 'NONE', #47609, #50824 ) ;
#57050=CARTESIAN_POINT ( 'NONE',  ( 34.92499999999998295, 22.22500000000000142, 4.500000000000000888 ) ) ;
#57052=ADVANCED_FACE ( 'NONE', ( #123373 ), #24738, .F. ) ;
#57053=FACE_OUTER_BOUND ( 'NONE', #107351, .T. ) ;
#57054=ORIENTED_EDGE ( 'NONE', *, *, #59601, .F. ) ;
#57056=ORIENTED_EDGE ( 'NONE', *, *, #97962, .F. ) ;
#57058=DIRECTION ( 'NONE',  ( -0.6830127018922180770, -0.6830127018922204085, -0.2588190451025213501 ) ) ;
#57059=FACE_OUTER_BOUND ( 'NONE', #64330, .T. ) ;
#57060=CARTESIAN_POINT ( 'NONE',  ( -26.99999999999981526, 14.87792677143806230, -11.06722581663446192 ) ) ;
#57061=EDGE_CURVE ( 'NONE', #81042, #104580, #55980, .T. ) ;
#57062=DIRECTION ( 'NONE',  ( -0.6830127018922180770, -0.6830127018922204085, -0.2588190451025213501 ) ) ;
#57064=PLANE ( 'NONE',  #130708 ) ;
#57067=CARTESIAN_POINT ( 'NONE',  ( 28.49999999999980815, 6.052185695429108669, 5.000000000000000000 ) ) ;
#57069=EDGE_LOOP ( 'NONE', ( #21703, #62585, #45073, #3900 ) ) ;
#57070=EDGE_LOOP ( 'NONE', ( #121784, #128114, #76219, #21650 ) ) ;
#57071=VERTEX_POINT ( 'NONE', #57396 ) ;
#57072=CARTESIAN_POINT ( 'NONE',  ( -13.49999999999990408, -8.947814304570734123, 5.000000000000000000 ) ) ;
#57074=VECTOR ( 'NONE', #51594, 1000.000000000000000 ) ;
#57075=CARTESIAN_POINT ( 'NONE',  ( 63.18398860626900415, 28.73617430169831621, 5.000000000000000000 ) ) ;
#57076=CARTESIAN_POINT ( 'NONE',  ( -48.18398860626899705, 28.73617430169820608, 5.000000000000000000 ) ) ;
#57078=DIRECTION ( 'NONE',  ( 0.7071067811865487940, -0.7071067811865463515, 0.000000000000000000 ) ) ;
#57079=CARTESIAN_POINT ( 'NONE',  ( -2.700255128608413990, -27.71228299555204089, 4.000000000000000000 ) ) ;
#57080=CARTESIAN_POINT ( 'NONE',  ( 2.292893218813447209, -15.74070752338412760, 5.000000000000000000 ) ) ;
#57081=DIRECTION ( 'NONE',  ( 0.000000000000000000, -1.000000000000000000, 0.000000000000000000 ) ) ;
#57082=DIRECTION ( 'NONE',  ( -0.000000000000000000, -0.3543493200069152693, 0.9351131265310292928 ) ) ;
#57084=EDGE_LOOP ( 'NONE', ( #136513, #65912, #143007, #106254 ) ) ;
#57086=ORIENTED_EDGE ( 'NONE', *, *, #7511, .T. ) ;
#57087=CARTESIAN_POINT ( 'NONE',  ( 0.000000000000000000, 0.000000000000000000, 5.000000000000000000 ) ) ;
#57088=DIRECTION ( 'NONE',  ( 0.7071067811865486830, -0.7071067811865464625, -0.000000000000000000 ) ) ;
#57089=ORIENTED_EDGE ( 'NONE', *, *, #6836, .F. ) ;
#57090=CARTESIAN_POINT ( 'NONE',  ( -11.51078643762690490, -27.52281430457047406, 5.000000000000000000 ) ) ;
#57091=DIRECTION ( 'NONE',  ( -0.000000000000000000, -0.3543493200069152693, 0.9351131265310292928 ) ) ;
#57092=EDGE_CURVE ( 'NONE', #40545, #67945, #133517, .T. ) ;
#57093=VERTEX_POINT ( 'NONE', #134234 ) ;
#57095=VERTEX_POINT ( 'NONE', #98722 ) ;
#57096=DIRECTION ( 'NONE',  ( -0.7071067811865486830, -0.7071067811865464625, -0.000000000000000000 ) ) ;
#57097=ORIENTED_EDGE ( 'NONE', *, *, #1736, .F. ) ;
#57100=ADVANCED_FACE ( 'NONE', ( #45115 ), #33514, .F. ) ;
#57105=VERTEX_POINT ( 'NONE', #46551 ) ;
#57106=ADVANCED_FACE ( 'NONE', ( #22564 ), #112473, .F. ) ;
#57110=ADVANCED_FACE ( 'NONE', ( #77715 ), #43642, .F. ) ;
#57111=CARTESIAN_POINT ( 'NONE',  ( -31.49999999999977973, -17.91344420646045776, 1.358650452708392242 ) ) ;
#57113=PLANE ( 'NONE',  #37513 ) ;
#57114=CARTESIAN_POINT ( 'NONE',  ( -5.999999999999963585, -11.35517001088073208, -1.126524801160121214 ) ) ;
#57115=EDGE_CURVE ( 'NONE', #115930, #119665, #87862, .T. ) ;
#57116=ORIENTED_EDGE ( 'NONE', *, *, #35087, .F. ) ;
#57117=ORIENTED_EDGE ( 'NONE', *, *, #142202, .F. ) ;
#57119=ADVANCED_FACE ( 'NONE', ( #56711 ), #68296, .F. ) ;
#57120=ORIENTED_EDGE ( 'NONE', *, *, #2904, .F. ) ;
#57121=AXIS2_PLACEMENT_3D ( 'NONE', #96865, #75193, #76619 ) ;
#57122=EDGE_CURVE ( 'NONE', #35940, #29609, #132101, .T. ) ;
#57124=LINE ( 'NONE', #11396, #140350 ) ;
#57125=CARTESIAN_POINT ( 'NONE',  ( 7.171830600776419651, -17.24070752338410273, 4.000000000000000000 ) ) ;
#57126=DIRECTION ( 'NONE',  ( 0.6830127018922181881, 0.6830127018922202975, -0.2588190451025214056 ) ) ;
#57128=ORIENTED_EDGE ( 'NONE', *, *, #5294, .F. ) ;
#57129=CARTESIAN_POINT ( 'NONE',  ( 48.48921356237309510, -27.52281430457089328, 5.000000000000000000 ) ) ;
#57130=DIRECTION ( 'NONE',  ( -0.7071067811865486830, -0.7071067811865464625, -0.000000000000000000 ) ) ;
#57132=DIRECTION ( 'NONE',  ( 0.6830127018922180770, -0.6830127018922204085, -0.2588190451025213501 ) ) ;
#57133=VECTOR ( 'NONE', #56281, 1000.000000000000000 ) ;
#57134=ORIENTED_EDGE ( 'NONE', *, *, #33706, .F. ) ;
#57135=EDGE_CURVE ( 'NONE', #95889, #102448, #13126, .T. ) ;
#57136=CARTESIAN_POINT ( 'NONE',  ( 42.48921356237308800, -27.52281430457085065, 5.000000000000000000 ) ) ;
#57137=DIRECTION ( 'NONE',  ( -0.6830127018922181881, 0.6830127018922202975, -0.2588190451025214056 ) ) ;
#57138=LINE ( 'NONE', #137528, #79888 ) ;
#57139=ORIENTED_EDGE ( 'NONE', *, *, #115124, .F. ) ;
#57140=CARTESIAN_POINT ( 'NONE',  ( 20.99451991528748707, 28.92564299267952777, 4.000000000000000000 ) ) ;
#57141=LINE ( 'NONE', #4084, #21548 ) ;
#57142=CARTESIAN_POINT ( 'NONE',  ( 0.000000000000000000, 0.000000000000000000, 5.000000000000000000 ) ) ;
#57144=VECTOR ( 'NONE', #113636, 1000.000000000000000 ) ;
#57145=LINE ( 'NONE', #131103, #49157 ) ;
#57147=ORIENTED_EDGE ( 'NONE', *, *, #109828, .F. ) ;
#57150=AXIS2_PLACEMENT_3D ( 'NONE', #45893, #88679, #43724 ) ;
#57152=VECTOR ( 'NONE', #116433, 1000.000000000000000 ) ;
#57153=VERTEX_POINT ( 'NONE', #6887 ) ;
#57154=FACE_OUTER_BOUND ( 'NONE', #68119, .T. ) ;
#57155=DIRECTION ( 'NONE',  ( -0.7071067811865486830, -0.7071067811865464625, -0.000000000000000000 ) ) ;
#57156=DIRECTION ( 'NONE',  ( 1.000000000000000000, 0.000000000000000000, 0.000000000000000000 ) ) ;
#57157=VECTOR ( 'NONE', #46423, 999.9999999999998863 ) ;
#57159=ORIENTED_EDGE ( 'NONE', *, *, #109795, .F. ) ;
#57160=PLANE ( 'NONE',  #106997 ) ;
#57161=LINE ( 'NONE', #4097, #11939 ) ;
#57162=CARTESIAN_POINT ( 'NONE',  ( -33.18398860626899705, 28.73617430169810305, 5.000000000000000000 ) ) ;
#57164=VERTEX_POINT ( 'NONE', #104814 ) ;
#57165=FACE_OUTER_BOUND ( 'NONE', #92063, .T. ) ;
#57166=ADVANCED_FACE ( 'NONE', ( #5478 ), #49757, .T. ) ;
#57167=PLANE ( 'NONE',  #40099 ) ;
#57168=ORIENTED_EDGE ( 'NONE', *, *, #80802, .F. ) ;
#57170=DIRECTION ( 'NONE',  ( -0.7071067811865486830, 0.7071067811865464625, 0.000000000000000000 ) ) ;
#57173=FACE_OUTER_BOUND ( 'NONE', #64809, .T. ) ;
#57174=ADVANCED_FACE ( 'NONE', ( #51165 ), #117798, .F. ) ;
#57175=CARTESIAN_POINT ( 'NONE',  ( -19.08335816409769237, -22.22500000000000142, -1.002990283292573004 ) ) ;
#57178=VERTEX_POINT ( 'NONE', #99638 ) ;
#57179=VERTEX_POINT ( 'NONE', #66337 ) ;
#57180=CARTESIAN_POINT ( 'NONE',  ( -36.18398860626899705, 28.73617430169812437, 5.000000000000000000 ) ) ;
#57181=ADVANCED_FACE ( 'NONE', ( #33713 ), #131578, .T. ) ;
#57182=EDGE_LOOP ( 'NONE', ( #31554, #89759, #33642, #124316 ) ) ;
#57183=ORIENTED_EDGE ( 'NONE', *, *, #20812, .T. ) ;
#57184=AXIS2_PLACEMENT_3D ( 'NONE', #98640, #32702, #131280 ) ;
#57185=FACE_OUTER_BOUND ( 'NONE', #140225, .T. ) ;
#57186=ORIENTED_EDGE ( 'NONE', *, *, #105646, .F. ) ;
#57187=LINE ( 'NONE', #2003, #89968 ) ;
#57189=EDGE_CURVE ( 'NONE', #5220, #66103, #31551, .T. ) ;
#57190=AXIS2_PLACEMENT_3D ( 'NONE', #6563, #138567, #81353 ) ;
#57192=CARTESIAN_POINT ( 'NONE',  ( 8.816011393731004731, 28.73617430169781173, 5.000000000000000000 ) ) ;
#57193=VERTEX_POINT ( 'NONE', #64903 ) ;
#57194=LINE ( 'NONE', #68085, #85827 ) ;
#57195=VECTOR ( 'NONE', #31137, 1000.000000000000000 ) ;
#57196=VERTEX_POINT ( 'NONE', #33012 ) ;
#57198=EDGE_CURVE ( 'NONE', #4623, #123033, #76500, .T. ) ;
#57199=ORIENTED_EDGE ( 'NONE', *, *, #101886, .T. ) ;
#57200=VERTEX_POINT ( 'NONE', #75081 ) ;
#57201=CARTESIAN_POINT ( 'NONE',  ( 9.299744871391588674, -27.71228299555212971, 4.000000000000000000 ) ) ;
#57202=EDGE_LOOP ( 'NONE', ( #107623, #132863, #75220, #9608 ) ) ;
#57203=ORIENTED_EDGE ( 'NONE', *, *, #116994, .T. ) ;
#57204=ORIENTED_EDGE ( 'NONE', *, *, #119757, .T. ) ;
#57205=VECTOR ( 'NONE', #141513, 999.9999999999998863 ) ;
#57206=CARTESIAN_POINT ( 'NONE',  ( 30.48921356237309510, -27.52281430457076894, 5.000000000000000000 ) ) ;
#57207=LINE ( 'NONE', #57924, #122409 ) ;
#57208=CARTESIAN_POINT ( 'NONE',  ( -42.29974487139158157, -27.71228299555235708, 4.000000000000000000 ) ) ;
#57209=VECTOR ( 'NONE', #56993, 1000.000000000000227 ) ;
#57211=DIRECTION ( 'NONE',  ( 0.7071067811865487940, -0.7071067811865463515, 0.000000000000000000 ) ) ;
#57212=DIRECTION ( 'NONE',  ( 0.7071067811865487940, -0.7071067811865463515, 0.000000000000000000 ) ) ;
#57213=CARTESIAN_POINT ( 'NONE',  ( -34.92460739249806068, 21.74787736706806029, 4.224371856075229026 ) ) ;
#57214=CARTESIAN_POINT ( 'NONE',  ( 0.000000000000000000, 0.000000000000000000, 5.000000000000000000 ) ) ;
#57216=VERTEX_POINT ( 'NONE', #77917 ) ;
#57218=CARTESIAN_POINT ( 'NONE',  ( 16.49999999999988276, -6.839392718269117211, -8.480912228396125130 ) ) ;
#57219=FACE_OUTER_BOUND ( 'NONE', #92236, .T. ) ;
#57220=ORIENTED_EDGE ( 'NONE', *, *, #119927, .F. ) ;
#57224=CYLINDRICAL_SURFACE ( 'NONE', #104698, 0.5000000000000004441 ) ;
#57225=DIRECTION ( 'NONE',  ( -0.7071067811865486830, -0.7071067811865464625, 0.000000000000000000 ) ) ;
#57226=CIRCLE ( 'NONE', #126611, 5.968999999999998529 ) ;
#57227=DIRECTION ( 'NONE',  ( -0.000000000000000000, 0.000000000000000000, 1.000000000000000000 ) ) ;
#57228=EDGE_CURVE ( 'NONE', #52039, #18836, #21390, .T. ) ;
#57229=DIRECTION ( 'NONE',  ( -0.7071067811865486830, -0.7071067811865464625, -0.000000000000000000 ) ) ;
#57230=ORIENTED_EDGE ( 'NONE', *, *, #141716, .F. ) ;
#57231=LINE ( 'NONE', #54379, #134363 ) ;
#57232=ORIENTED_EDGE ( 'NONE', *, *, #58807, .T. ) ;
#57233=VECTOR ( 'NONE', #57523, 1000.000000000000000 ) ;
#57235=VECTOR ( 'NONE', #35776, 1000.000000000000000 ) ;
#57236=PLANE ( 'NONE',  #9748 ) ;
#57239=EDGE_LOOP ( 'NONE', ( #69702, #93205, #56674, #6163 ) ) ;
#57241=DIRECTION ( 'NONE',  ( -0.6830127018922180770, 0.6830127018922202975, -0.2588190451025213501 ) ) ;
#57242=FACE_OUTER_BOUND ( 'NONE', #139939, .T. ) ;
#57243=ORIENTED_EDGE ( 'NONE', *, *, #52351, .F. ) ;
#57244=VECTOR ( 'NONE', #25175, 999.9999999999998863 ) ;
#57247=LINE ( 'NONE', #69544, #12521 ) ;
#57249=VECTOR ( 'NONE', #129861, 1000.000000000000000 ) ;
#57250=CARTESIAN_POINT ( 'NONE',  ( 6.299744871391586898, -27.71228299555210484, 4.000000000000000000 ) ) ;
#57251=LINE ( 'NONE', #677, #88982 ) ;
#57253=EDGE_LOOP ( 'NONE', ( #27076, #20738, #106578, #55900 ) ) ;
#57254=CARTESIAN_POINT ( 'NONE',  ( 48.18398860626899705, 28.73617430169820608, 5.000000000000000000 ) ) ;
#57257=ORIENTED_EDGE ( 'NONE', *, *, #27205, .T. ) ;
#57258=LINE ( 'NONE', #67417, #135011 ) ;
#57259=ORIENTED_EDGE ( 'NONE', *, *, #36955, .T. ) ;
#57260=( BOUNDED_CURVE ( )  B_SPLINE_CURVE ( 3, ( #17149, #15666, #136773, #97344 ),
 .UNSPECIFIED., .F., .F. ) 
 B_SPLINE_CURVE_WITH_KNOTS ( ( 4, 4 ),
 ( 6.095931195673057523, 6.243513561394028244 ),
 .UNSPECIFIED. ) 
 CURVE ( )  GEOMETRIC_REPRESENTATION_ITEM ( )  RATIONAL_B_SPLINE_CURVE ( ( 1.000000000000000000, 0.9981857772260753769, 0.9981857772260753769, 1.000000000000000000 ) ) 
 REPRESENTATION_ITEM ( '' )  );
#57262=ORIENTED_EDGE ( 'NONE', *, *, #28072, .T. ) ;
#57264=LINE ( 'NONE', #88456, #23907 ) ;
#57265=CARTESIAN_POINT ( 'NONE',  ( 0.000000000000000000, 0.000000000000000000, 5.000000000000000000 ) ) ;
#57266=VECTOR ( 'NONE', #46162, 1000.000000000000000 ) ;
#57267=ORIENTED_EDGE ( 'NONE', *, *, #38259, .F. ) ;
#57269=ORIENTED_EDGE ( 'NONE', *, *, #98575, .F. ) ;
#57270=DIRECTION ( 'NONE',  ( -0.000000000000000000, -0.3543493200069152693, 0.9351131265310292928 ) ) ;
#57271=LINE ( 'NONE', #35530, #131862 ) ;
#57272=EDGE_CURVE ( 'NONE', #108649, #124601, #310, .T. ) ;
#57273=VECTOR ( 'NONE', #16862, 1000.000000000000000 ) ;
#57274=DIRECTION ( 'NONE',  ( -0.6830127018922180770, -0.6830127018922204085, -0.2588190451025213501 ) ) ;
#57277=DIRECTION ( 'NONE',  ( 0.3543493200069162685, -0.000000000000000000, -0.9351131265310288487 ) ) ;
#57278=CARTESIAN_POINT ( 'NONE',  ( -18.18398860626898994, 28.73617430169800002, 5.000000000000000000 ) ) ;
#57279=CARTESIAN_POINT ( 'NONE',  ( 9.183988606268997046, 28.73617430169793607, 5.000000000000000000 ) ) ;
#57280=EDGE_CURVE ( 'NONE', #99958, #96272, #108343, .T. ) ;
#57283=LINE ( 'NONE', #36225, #44458 ) ;
#57284=VECTOR ( 'NONE', #130239, 1000.000000000000000 ) ;
#57285=CARTESIAN_POINT ( 'NONE',  ( 19.49999999999986144, -14.56887692260766443, 4.000000000000000000 ) ) ;
#57286=PLANE ( 'NONE',  #32816 ) ;
#57287=LINE ( 'NONE', #79044, #57157 ) ;
#57288=EDGE_CURVE ( 'NONE', #88886, #84730, #119246, .T. ) ;
#57289=ORIENTED_EDGE ( 'NONE', *, *, #37249, .F. ) ;
#57290=ORIENTED_EDGE ( 'NONE', *, *, #24659, .T. ) ;
#57292=ORIENTED_EDGE ( 'NONE', *, *, #14729, .T. ) ;
#57293=ORIENTED_EDGE ( 'NONE', *, *, #131975, .F. ) ;
#57294=ORIENTED_EDGE ( 'NONE', *, *, #94737, .T. ) ;
#57295=VECTOR ( 'NONE', #115886, 1000.000000000000000 ) ;
#57296=DIRECTION ( 'NONE',  ( 0.7071067811865487940, 0.7071067811865463515, -0.000000000000000000 ) ) ;
#57299=ORIENTED_EDGE ( 'NONE', *, *, #102468, .T. ) ;
#57300=DIRECTION ( 'NONE',  ( -0.000000000000000000, 0.3543493200069153248, 0.9351131265310292928 ) ) ;
#57302=EDGE_CURVE ( 'NONE', #110142, #126713, #11173, .T. ) ;
#57303=PLANE ( 'NONE',  #139053 ) ;
#57304=DIRECTION ( 'NONE',  ( 0.6830127018922181881, 0.6830127018922202975, -0.2588190451025214056 ) ) ;
#57305=ADVANCED_FACE ( 'NONE', ( #100383 ), #65651, .F. ) ;
#57307=LINE ( 'NONE', #86529, #2990 ) ;
#57308=LINE ( 'NONE', #99321, #61276 ) ;
#57309=DIRECTION ( 'NONE',  ( -0.7071067811865486830, -0.7071067811865464625, -0.000000000000000000 ) ) ;
#57310=CARTESIAN_POINT ( 'NONE',  ( 34.42499999999998295, 22.22500000000000142, 5.000000000000000000 ) ) ;
#57311=FACE_OUTER_BOUND ( 'NONE', #113621, .T. ) ;
#57313=EDGE_CURVE ( 'NONE', #16774, #55512, #111221, .T. ) ;
#57314=CARTESIAN_POINT ( 'NONE',  ( -14.99999999999989164, -13.06887692260767686, 4.000000000000000000 ) ) ;
#57315=VERTEX_POINT ( 'NONE', #9780 ) ;
#57316=VERTEX_POINT ( 'NONE', #109817 ) ;
#57318=VERTEX_POINT ( 'NONE', #22762 ) ;
#57319=LINE ( 'NONE', #66745, #110307 ) ;
#57320=ADVANCED_FACE ( 'NONE', ( #88803 ), #11915, .F. ) ;
#57321=FACE_OUTER_BOUND ( 'NONE', #86801, .T. ) ;
#57322=LINE ( 'NONE', #2896, #25764 ) ;
#57325=ORIENTED_EDGE ( 'NONE', *, *, #59479, .T. ) ;
#57326=ORIENTED_EDGE ( 'NONE', *, *, #75299, .F. ) ;
#57327=ADVANCED_FACE ( 'NONE', ( #56201 ), #89489, .T. ) ;
#57328=CARTESIAN_POINT ( 'NONE',  ( 51.18398860626899705, 28.73617430169823095, 5.000000000000000000 ) ) ;
#57329=VECTOR ( 'NONE', #3484, 1000.000000000000000 ) ;
#57330=ORIENTED_EDGE ( 'NONE', *, *, #34211, .T. ) ;
#57331=ORIENTED_EDGE ( 'NONE', *, *, #33113, .F. ) ;
#57332=VECTOR ( 'NONE', #24332, 1000.000000000000000 ) ;
#57334=DIRECTION ( 'NONE',  ( -0.000000000000000000, 0.000000000000000000, 1.000000000000000000 ) ) ;
#57337=AXIS2_PLACEMENT_3D ( 'NONE', #90490, #35433, #24509 ) ;
#57338=EDGE_CURVE ( 'NONE', #57318, #127365, #134443, .T. ) ;
#57339=VECTOR ( 'NONE', #72492, 1000.000000000000227 ) ;
#57340=LINE ( 'NONE', #2166, #19921 ) ;
#57341=VERTEX_POINT ( 'NONE', #25656 ) ;
#57342=ORIENTED_EDGE ( 'NONE', *, *, #86334, .F. ) ;
#57343=DIRECTION ( 'NONE',  ( -0.7071067811865487940, 0.7071067811865463515, 0.000000000000000000 ) ) ;
#57344=ORIENTED_EDGE ( 'NONE', *, *, #51805, .T. ) ;
#57345=VERTEX_POINT ( 'NONE', #69931 ) ;
#57346=VECTOR ( 'NONE', #33095, 1000.000000000000000 ) ;
#57347=ORIENTED_EDGE ( 'NONE', *, *, #51805, .F. ) ;
#57348=FACE_OUTER_BOUND ( 'NONE', #107644, .T. ) ;
#57350=CARTESIAN_POINT ( 'NONE',  ( -11.99999999999990052, -19.44781430457063465, 5.000000000000000000 ) ) ;
#57351=ORIENTED_EDGE ( 'NONE', *, *, #135630, .T. ) ;
#57352=FACE_OUTER_BOUND ( 'NONE', #20250, .T. ) ;
#57353=EDGE_CURVE ( 'NONE', #44653, #79735, #136551, .T. ) ;
#57354=DIRECTION ( 'NONE',  ( 0.7071067811865487940, 0.7071067811865463515, 0.000000000000000000 ) ) ;
#57355=DIRECTION ( 'NONE',  ( 0.7071067811865487940, 0.7071067811865463515, 0.000000000000000000 ) ) ;
#57356=FACE_BOUND ( 'NONE', #113143, .T. ) ;
#57357=ORIENTED_EDGE ( 'NONE', *, *, #108238, .F. ) ;
#57358=CARTESIAN_POINT ( 'NONE',  ( -27.85181644961838288, 17.25929247661554200, 8.802941693769138709 ) ) ;
#57359=LINE ( 'NONE', #46510, #69306 ) ;
#57360=EDGE_CURVE ( 'NONE', #48401, #14592, #90200, .T. ) ;
#57362=DIRECTION ( 'NONE',  ( -0.7071067811865486830, -0.7071067811865464625, 0.000000000000000000 ) ) ;
#57363=EDGE_LOOP ( 'NONE', ( #143355, #24529, #140760, #77107 ) ) ;
#57364=CARTESIAN_POINT ( 'NONE',  ( -17.11087965568911073, 8.820243421702873121, 4.000000000000000000 ) ) ;
#57365=EDGE_LOOP ( 'NONE', ( #89779, #109886, #32070, #44470, #101772 ) ) ;
#57366=VECTOR ( 'NONE', #59033, 1000.000000000000114 ) ;
#57367=ORIENTED_EDGE ( 'NONE', *, *, #137972, .F. ) ;
#57368=ORIENTED_EDGE ( 'NONE', *, *, #28249, .T. ) ;
#57372=DIRECTION ( 'NONE',  ( -0.3543493200069162685, -0.000000000000000000, -0.9351131265310288487 ) ) ;
#57373=EDGE_CURVE ( 'NONE', #30354, #24532, #12633, .T. ) ;
#57374=ORIENTED_EDGE ( 'NONE', *, *, #46889, .T. ) ;
#57375=DIRECTION ( 'NONE',  ( -0.3543493200069162685, -0.000000000000000000, -0.9351131265310288487 ) ) ;
#57376=CARTESIAN_POINT ( 'NONE',  ( -33.32816939922329880, 11.25929247661560062, 4.000000000000000000 ) ) ;
#57377=CARTESIAN_POINT ( 'NONE',  ( 3.489213562373097322, -27.52281430457057709, 5.000000000000000000 ) ) ;
#57381=ORIENTED_EDGE ( 'NONE', *, *, #108237, .T. ) ;
#57383=VERTEX_POINT ( 'NONE', #103212 ) ;
#57385=CARTESIAN_POINT ( 'NONE',  ( 2.994519915287485734, 28.92564299267940342, 4.000000000000000000 ) ) ;
#57386=ORIENTED_EDGE ( 'NONE', *, *, #86125, .T. ) ;
#57387=VERTEX_POINT ( 'NONE', #101071 ) ;
#57388=CARTESIAN_POINT ( 'NONE',  ( -34.92500000000001137, -22.22500000000000142, 4.500000000000000888 ) ) ;
#57389=EDGE_CURVE ( 'NONE', #54369, #128989, #3864, .T. ) ;
#57390=ADVANCED_FACE ( 'NONE', ( #125712 ), #26393, .F. ) ;
#57391=PLANE ( 'NONE',  #55542 ) ;
#57392=ORIENTED_EDGE ( 'NONE', *, *, #95935, .T. ) ;
#57393=CARTESIAN_POINT ( 'NONE',  ( 51.18398860626899705, 28.73617430169823095, 5.000000000000000000 ) ) ;
#57396=CARTESIAN_POINT ( 'NONE',  ( -22.49999999999984013, -4.912538124160710673, 4.000000000000000000 ) ) ;
#57397=EDGE_LOOP ( 'NONE', ( #51384, #38876, #110628, #127791 ) ) ;
#57399=DIRECTION ( 'NONE',  ( 0.7071067811865487940, 0.7071067811865463515, 0.000000000000000000 ) ) ;
#57401=CARTESIAN_POINT ( 'NONE',  ( 22.49999999999983658, -14.94781430457066840, 5.000000000000000000 ) ) ;
#57402=DIRECTION ( 'NONE',  ( 0.7071067811865487940, 0.7071067811865463515, -0.000000000000000000 ) ) ;
#57403=ORIENTED_EDGE ( 'NONE', *, *, #143285, .F. ) ;
#57404=DIRECTION ( 'NONE',  ( 0.7071067811865487940, -0.7071067811865463515, 0.000000000000000000 ) ) ;
#57405=DIRECTION ( 'NONE',  ( -1.000000000000000000, 0.000000000000000000, -0.000000000000000000 ) ) ;
#57407=CARTESIAN_POINT ( 'NONE',  ( 2.999999999999978240, -10.06887692260771416, 4.000000000000000000 ) ) ;
#57408=EDGE_LOOP ( 'NONE', ( #135337, #136496, #81121 ) ) ;
#57409=CARTESIAN_POINT ( 'NONE',  ( 63.18398860626900415, 28.73617430169831621, 5.000000000000000000 ) ) ;
#57411=DIRECTION ( 'NONE',  ( -0.7071067811865487940, 0.7071067811865463515, -0.000000000000000000 ) ) ;
#57413=EDGE_CURVE ( 'NONE', #7339, #136825, #13338, .T. ) ;
#57415=DIRECTION ( 'NONE',  ( 0.3543493200069163240, -0.000000000000000000, 0.9351131265310288487 ) ) ;
#57416=VECTOR ( 'NONE', #111081, 1000.000000000000000 ) ;
#57417=LINE ( 'NONE', #87879, #78935 ) ;
#57418=CARTESIAN_POINT ( 'NONE',  ( 69.48921356237309510, -27.52281430457103895, 5.000000000000000000 ) ) ;
#57419=ORIENTED_EDGE ( 'NONE', *, *, #80195, .T. ) ;
#57420=VECTOR ( 'NONE', #133705, 1000.000000000000000 ) ;
#57421=DIRECTION ( 'NONE',  ( 0.7071067811865486830, -0.7071067811865464625, -0.000000000000000000 ) ) ;
#57422=ORIENTED_EDGE ( 'NONE', *, *, #137776, .T. ) ;
#57423=VECTOR ( 'NONE', #138822, 1000.000000000000227 ) ;
#57424=LINE ( 'NONE', #66156, #141053 ) ;
#57425=LINE ( 'NONE', #13863, #34852 ) ;
#57426=ORIENTED_EDGE ( 'NONE', *, *, #36689, .T. ) ;
#57427=ORIENTED_EDGE ( 'NONE', *, *, #47299, .F. ) ;
#57429=CARTESIAN_POINT ( 'NONE',  ( -0.2997448713915885632, -27.71228299555206220, 4.000000000000000000 ) ) ;
#57430=VECTOR ( 'NONE', #5959, 1000.000000000000000 ) ;
#57431=EDGE_LOOP ( 'NONE', ( #6411, #56355, #73397, #125142 ) ) ;
#57432=AXIS2_PLACEMENT_3D ( 'NONE', #32011, #79127, #66789 ) ;
#57433=( BOUNDED_CURVE ( )  B_SPLINE_CURVE ( 3, ( #103247, #15495, #14090, #93101 ),
 .UNSPECIFIED., .F., .T. ) 
 B_SPLINE_CURVE_WITH_KNOTS ( ( 4, 4 ),
 ( 4.350170835173026163, 4.500739107949204509 ),
 .UNSPECIFIED. ) 
 CURVE ( )  GEOMETRIC_REPRESENTATION_ITEM ( )  RATIONAL_B_SPLINE_CURVE ( ( 1.000000000000000000, 0.9981116584018959736, 0.9981116584018959736, 1.000000000000000000 ) ) 
 REPRESENTATION_ITEM ( '' )  );
#57434=LINE ( 'NONE', #857, #62205 ) ;
#57435=EDGE_CURVE ( 'NONE', #91556, #111517, #15459, .T. ) ;
#57438=EDGE_CURVE ( 'NONE', #25811, #45676, #59747, .T. ) ;
#57439=PLANE ( 'NONE',  #53608 ) ;
#57440=CARTESIAN_POINT ( 'NONE',  ( -5.004924772211909456, -5.240707523384228850, 12.38332538355497192 ) ) ;
#57442=CARTESIAN_POINT ( 'NONE',  ( -8.999999999999934275, -11.35517001088073208, -1.126524801160128986 ) ) ;
#57444=PLANE ( 'NONE',  #58198 ) ;
#57445=ADVANCED_FACE ( 'NONE', ( #122839 ), #23515, .T. ) ;
#57446=ORIENTED_EDGE ( 'NONE', *, *, #62982, .F. ) ;
#57447=EDGE_CURVE ( 'NONE', #15104, #34146, #117068, .T. ) ;
#57449=EDGE_LOOP ( 'NONE', ( #55733, #80428, #83381, #10467 ) ) ;
#57450=CARTESIAN_POINT ( 'NONE',  ( 23.99999999999983302, 12.25461709320622639, -10.07315571508691754 ) ) ;
#57451=VERTEX_POINT ( 'NONE', #69186 ) ;
#57452=ORIENTED_EDGE ( 'NONE', *, *, #136770, .F. ) ;
#57453=ORIENTED_EDGE ( 'NONE', *, *, #93635, .F. ) ;
#57454=CARTESIAN_POINT ( 'NONE',  ( -17.99999999999986855, 7.007997736742429318, -8.085015511992153847 ) ) ;
#57455=FACE_OUTER_BOUND ( 'NONE', #44532, .T. ) ;
#57457=DIRECTION ( 'NONE',  ( 0.3543493200069162685, -0.000000000000000000, -0.9351131265310288487 ) ) ;
#57458=PLANE ( 'NONE',  #90619 ) ;
#57459=VECTOR ( 'NONE', #137441, 1000.000000000000000 ) ;
#57460=CARTESIAN_POINT ( 'NONE',  ( 39.18398860626899705, 28.73617430169814568, 5.000000000000000000 ) ) ;
#57461=EDGE_CURVE ( 'NONE', #142771, #138853, #3186, .T. ) ;
#57462=CARTESIAN_POINT ( 'NONE',  ( -7.828169399223472880, -2.240707523384257716, 4.000000000000000000 ) ) ;
#57464=ORIENTED_EDGE ( 'NONE', *, *, #12357, .F. ) ;
#57465=EDGE_CURVE ( 'NONE', #6381, #29382, #36541, .T. ) ;
#57466=CARTESIAN_POINT ( 'NONE',  ( 20.84387692260743918, -22.22500000000000142, 4.000000000000000000 ) ) ;
#57468=VECTOR ( 'NONE', #10951, 1000.000000000000000 ) ;
#57469=CARTESIAN_POINT ( 'NONE',  ( -5.671830600776431197, -3.740707523384244837, 4.000000000000000000 ) ) ;
#57471=LINE ( 'NONE', #37114, #70677 ) ;
#57472=DIRECTION ( 'NONE',  ( -0.7071067811865486830, -0.7071067811865464625, 0.000000000000000000 ) ) ;
#57475=CARTESIAN_POINT ( 'NONE',  ( -26.20710678118635428, 6.759292476615649470, 5.000000000000000000 ) ) ;
#57477=ORIENTED_EDGE ( 'NONE', *, *, #56773, .F. ) ;
#57478=ORIENTED_EDGE ( 'NONE', *, *, #26490, .F. ) ;
#57480=EDGE_CURVE ( 'NONE', #111351, #126851, #95912, .T. ) ;
#57481=VERTEX_POINT ( 'NONE', #49596 ) ;
#57483=ORIENTED_EDGE ( 'NONE', *, *, #89955, .T. ) ;
#57484=ADVANCED_FACE ( 'NONE', ( #117631 ), #116950, .F. ) ;
#57485=VECTOR ( 'NONE', #31512, 1000.000000000000000 ) ;
#57486=LINE ( 'NONE', #3069, #50192 ) ;
#57487=CARTESIAN_POINT ( 'NONE',  ( -42.18398860626899705, 28.73617430169816700, 5.000000000000000000 ) ) ;
#57490=ORIENTED_EDGE ( 'NONE', *, *, #133702, .T. ) ;
#57491=CARTESIAN_POINT ( 'NONE',  ( -11.99999999999991296, -10.44781430457072346, 5.000000000000000000 ) ) ;
#57492=ORIENTED_EDGE ( 'NONE', *, *, #130568, .T. ) ;
#57493=EDGE_CURVE ( 'NONE', #47109, #120574, #40150, .T. ) ;
#57494=CARTESIAN_POINT ( 'NONE',  ( 32.99451991528749062, 28.92564299267960948, 4.000000000000000000 ) ) ;
#57495=FACE_OUTER_BOUND ( 'NONE', #48042, .T. ) ;
#57496=ORIENTED_EDGE ( 'NONE', *, *, #96037, .F. ) ;
#57497=CARTESIAN_POINT ( 'NONE',  ( -14.95341186370446884, 14.25929247661557753, 18.84478104361331674 ) ) ;
#57498=ORIENTED_EDGE ( 'NONE', *, *, #113931, .F. ) ;
#57499=PLANE ( 'NONE',  #81837 ) ;
#57500=CARTESIAN_POINT ( 'NONE',  ( -27.48921356237309155, -27.52281430457074762, 5.000000000000000000 ) ) ;
#57501=CARTESIAN_POINT ( 'NONE',  ( -34.17183060077623225, 15.75929247661555443, 4.000000000000000000 ) ) ;
#57502=EDGE_CURVE ( 'NONE', #91612, #106637, #28537, .T. ) ;
#57503=EDGE_CURVE ( 'NONE', #46830, #96047, #85036, .T. ) ;
#57504=CARTESIAN_POINT ( 'NONE',  ( -11.99999999999990941, -9.412538124160661823, 4.000000000000000000 ) ) ;
#57505=CARTESIAN_POINT ( 'NONE',  ( 15.67180000000000639, 3.174999999999997602, 0.000000000000000000 ) ) ;
#57506=EDGE_CURVE ( 'NONE', #91733, #9906, #138006, .T. ) ;
#57507=VERTEX_POINT ( 'NONE', #93779 ) ;
#57511=LINE ( 'NONE', #34308, #34847 ) ;
#57512=CARTESIAN_POINT ( 'NONE',  ( 33.32816939922329880, -12.74070752338415247, 4.000000000000000000 ) ) ;
#57513=DIRECTION ( 'NONE',  ( 0.7071067811865487940, 0.7071067811865463515, -0.000000000000000000 ) ) ;
#57514=ORIENTED_EDGE ( 'NONE', *, *, #122647, .F. ) ;
#57515=ORIENTED_EDGE ( 'NONE', *, *, #17599, .T. ) ;
#57518=ORIENTED_EDGE ( 'NONE', *, *, #2802, .F. ) ;
#57519=VECTOR ( 'NONE', #11708, 1000.000000000000000 ) ;
#57520=FACE_OUTER_BOUND ( 'NONE', #110993, .T. ) ;
#57521=ORIENTED_EDGE ( 'NONE', *, *, #55004, .T. ) ;
#57522=DIRECTION ( 'NONE',  ( -0.000000000000000000, 0.000000000000000000, 1.000000000000000000 ) ) ;
#57523=DIRECTION ( 'NONE',  ( -0.000000000000000000, -0.3543493200069152693, 0.9351131265310292928 ) ) ;
#57524=CARTESIAN_POINT ( 'NONE',  ( 3.328169399223511515, 20.25929247661551713, 4.000000000000000000 ) ) ;
#57525=VECTOR ( 'NONE', #6279, 1000.000000000000000 ) ;
#57529=FACE_BOUND ( 'NONE', #124413, .T. ) ;
#57530=LINE ( 'NONE', #101718, #94207 ) ;
#57531=LINE ( 'NONE', #91566, #14214 ) ;
#57532=LINE ( 'NONE', #124190, #34143 ) ;
#57533=DIRECTION ( 'NONE',  ( 0.7071067811865487940, -0.7071067811865463515, 0.000000000000000000 ) ) ;
#57534=VERTEX_POINT ( 'NONE', #105353 ) ;
#57535=AXIS2_PLACEMENT_3D ( 'NONE', #37764, #92826, #113139 ) ;
#57536=ORIENTED_EDGE ( 'NONE', *, *, #38250, .F. ) ;
#57538=CARTESIAN_POINT ( 'NONE',  ( -32.20710678118631165, -8.240707523384193323, 5.000000000000000000 ) ) ;
#57542=ORIENTED_EDGE ( 'NONE', *, *, #9549, .F. ) ;
#57544=ADVANCED_FACE ( 'NONE', ( #38690 ), #19066, .T. ) ;
#57545=EDGE_LOOP ( 'NONE', ( #66116, #27560, #32441 ) ) ;
#57546=PLANE ( 'NONE',  #88390 ) ;
#57548=LINE ( 'NONE', #11849, #130616 ) ;
#57551=CARTESIAN_POINT ( 'NONE',  ( 34.42499999999998295, 8.977185695429312773, 5.000000000000000000 ) ) ;
#57552=FACE_OUTER_BOUND ( 'NONE', #40522, .T. ) ;
#57556=ORIENTED_EDGE ( 'NONE', *, *, #73686, .T. ) ;
#57558=CARTESIAN_POINT ( 'NONE',  ( -18.28838880452753202, -2.745211937670052560, 5.000000000000000000 ) ) ;
#57559=DIRECTION ( 'NONE',  ( 1.000000000000000000, 0.000000000000000000, 0.000000000000000000 ) ) ;
#57561=AXIS2_PLACEMENT_3D ( 'NONE', #143154, #86658, #54049 ) ;
#57562=ORIENTED_EDGE ( 'NONE', *, *, #11337, .T. ) ;
#57563=AXIS2_PLACEMENT_3D ( 'NONE', #18083, #52178, #120248 ) ;
#57564=VERTEX_POINT ( 'NONE', #106774 ) ;
#57565=ADVANCED_FACE ( 'NONE', ( #84363 ), #7453, .T. ) ;
#57566=EDGE_CURVE ( 'NONE', #100222, #84831, #51719, .T. ) ;
#57568=EDGE_LOOP ( 'NONE', ( #60693, #126163, #78540, #55238 ) ) ;
#57570=ADVANCED_FACE ( 'NONE', ( #61888 ), #106047, .F. ) ;
#57571=CARTESIAN_POINT ( 'NONE',  ( -21.48921356237309155, -27.52281430457070499, 5.000000000000000000 ) ) ;
#57573=CARTESIAN_POINT ( 'NONE',  ( 18.70701326429291456, -21.74070752338405654, 4.999753212805210012 ) ) ;
#57574=ORIENTED_EDGE ( 'NONE', *, *, #124872, .F. ) ;
#57575=ADVANCED_FACE ( 'NONE', ( #95190 ), #72068, .F. ) ;
#57576=PLANE ( 'NONE',  #17874 ) ;
#57578=LINE ( 'NONE', #23488, #93842 ) ;
#57580=CARTESIAN_POINT ( 'NONE',  ( 7.171830600776432973, 21.75929247661550647, 4.000000000000000000 ) ) ;
#57581=ORIENTED_EDGE ( 'NONE', *, *, #3332, .F. ) ;
#57582=VERTEX_POINT ( 'NONE', #74174 ) ;
#57584=LINE ( 'NONE', #66311, #53881 ) ;
#57588=ORIENTED_EDGE ( 'NONE', *, *, #93089, .T. ) ;
#57590=CARTESIAN_POINT ( 'NONE',  ( -45.48921356237309510, -27.52281430457087197, 5.000000000000000000 ) ) ;
#57593=CARTESIAN_POINT ( 'NONE',  ( 1.499999999999997780, -11.94781430457070925, 5.000000000000000000 ) ) ;
#57594=EDGE_CURVE ( 'NONE', #19920, #105277, #137296, .T. ) ;
#57595=DIRECTION ( 'NONE',  ( 0.000000000000000000, 1.000000000000000000, 0.000000000000000000 ) ) ;
#57596=LINE ( 'NONE', #47461, #12278 ) ;
#57597=CARTESIAN_POINT ( 'NONE',  ( -34.92500000000001137, 20.18441419595454889, 5.773254242255872803 ) ) ;
#57598=DIRECTION ( 'NONE',  ( -0.000000000000000000, -0.3543493200069152693, 0.9351131265310292928 ) ) ;
#57599=CARTESIAN_POINT ( 'NONE',  ( -31.82816939922330235, 18.75929247661553134, 4.000000000000000000 ) ) ;
#57600=ORIENTED_EDGE ( 'NONE', *, *, #30070, .T. ) ;
#57601=ORIENTED_EDGE ( 'NONE', *, *, #9618, .F. ) ;
#57602=EDGE_CURVE ( 'NONE', #123479, #19313, #116242, .T. ) ;
#57604=DIRECTION ( 'NONE',  ( -0.7071067811865486830, 0.7071067811865464625, 0.000000000000000000 ) ) ;
#57605=FACE_OUTER_BOUND ( 'NONE', #44021, .T. ) ;
#57607=CARTESIAN_POINT ( 'NONE',  ( 4.553349423367797577, 2.259292476615694323, 14.86850063742353356 ) ) ;
#57608=ORIENTED_EDGE ( 'NONE', *, *, #96621, .F. ) ;
#57609=CARTESIAN_POINT ( 'NONE',  ( 24.79289321881328689, -8.240707523384202204, 5.000000000000000000 ) ) ;
#57610=CARTESIAN_POINT ( 'NONE',  ( -6.707106781186496391, 11.25929247661560595, 5.000000000000000000 ) ) ;
#57612=ORIENTED_EDGE ( 'NONE', *, *, #47132, .T. ) ;
#57614=CARTESIAN_POINT ( 'NONE',  ( -28.49999999999980460, -14.56887692260766443, 4.000000000000000000 ) ) ;
#57615=CARTESIAN_POINT ( 'NONE',  ( 48.48921356237309510, -27.52281430457089328, 5.000000000000000000 ) ) ;
#57617=CARTESIAN_POINT ( 'NONE',  ( -18.29974487139159223, -27.71228299555219010, 4.000000000000000000 ) ) ;
#57618=EDGE_CURVE ( 'NONE', #138855, #94977, #66164, .T. ) ;
#57619=EDGE_CURVE ( 'NONE', #6418, #77362, #65463, .T. ) ;
#57620=VECTOR ( 'NONE', #120290, 1000.000000000000227 ) ;
#57621=DIRECTION ( 'NONE',  ( 0.7071067811865487940, 0.7071067811865463515, 0.000000000000000000 ) ) ;
#57622=ORIENTED_EDGE ( 'NONE', *, *, #4901, .T. ) ;
#57623=DIRECTION ( 'NONE',  ( 0.7071067811865487940, -0.7071067811865463515, 0.000000000000000000 ) ) ;
#57624=ORIENTED_EDGE ( 'NONE', *, *, #20804, .T. ) ;
#57625=CARTESIAN_POINT ( 'NONE',  ( -14.16347128873441896, 15.75929247661555443, 9.299976744542886919 ) ) ;
#57627=VECTOR ( 'NONE', #3340, 1000.000000000000114 ) ;
#57628=VECTOR ( 'NONE', #87636, 1000.000000000000000 ) ;
#57630=DIRECTION ( 'NONE',  ( -0.6830127018922180770, -0.6830127018922204085, -0.2588190451025213501 ) ) ;
#57631=PLANE ( 'NONE',  #111384 ) ;
#57634=EDGE_CURVE ( 'NONE', #91413, #15309, #131411, .T. ) ;
#57637=VERTEX_POINT ( 'NONE', #129979 ) ;
#57638=ORIENTED_EDGE ( 'NONE', *, *, #65026, .F. ) ;
#57639=CARTESIAN_POINT ( 'NONE',  ( 32.99999999999977973, -10.44781430457071458, 5.000000000000000000 ) ) ;
#57642=CIRCLE ( 'NONE', #43748, 3.378199999999994319 ) ;
#57643=VECTOR ( 'NONE', #93781, 1000.000000000000227 ) ;
#57644=DIRECTION ( 'NONE',  ( 0.7071067811865486830, -0.7071067811865464625, -0.000000000000000000 ) ) ;
#57645=LINE ( 'NONE', #136587, #55024 ) ;
#57647=CARTESIAN_POINT ( 'NONE',  ( 3.792893218813431222, 12.75929247661559351, 5.000000000000000000 ) ) ;
#57648=DIRECTION ( 'NONE',  ( -0.000000000000000000, -0.000000000000000000, 1.000000000000000000 ) ) ;
#57651=EDGE_CURVE ( 'NONE', #127842, #142744, #106035, .T. ) ;
#57652=PLANE ( 'NONE',  #47053 ) ;
#57653=PLANE ( 'NONE',  #122614 ) ;
#57654=CARTESIAN_POINT ( 'NONE',  ( -31.49999999999977973, 10.08746187583914811, 4.000000000000000000 ) ) ;
#57657=ORIENTED_EDGE ( 'NONE', *, *, #66929, .F. ) ;
#57658=EDGE_CURVE ( 'NONE', #16129, #107875, #32090, .T. ) ;
#57659=( BOUNDED_CURVE ( )  B_SPLINE_CURVE ( 3, ( #9090, #52635, #31619, #119313 ),
 .UNSPECIFIED., .F., .F. ) 
 B_SPLINE_CURVE_WITH_KNOTS ( ( 4, 4 ),
 ( 5.143245962375971203, 6.645403452391246191 ),
 .UNSPECIFIED. ) 
 CURVE ( )  GEOMETRIC_REPRESENTATION_ITEM ( )  RATIONAL_B_SPLINE_CURVE ( ( 1.000000000000000000, 0.8206354192515254997, 0.8206354192515254997, 1.000000000000000000 ) ) 
 REPRESENTATION_ITEM ( '' )  );
#57660=CARTESIAN_POINT ( 'NONE',  ( -22.59167451900985668, -0.7407075233842665973, 14.76736230305375130 ) ) ;
#57661=VECTOR ( 'NONE', #65694, 1000.000000000000227 ) ;
#57664=DIRECTION ( 'NONE',  ( -0.7071067811865486830, -0.7071067811865464625, 0.000000000000000000 ) ) ;
#57665=ORIENTED_EDGE ( 'NONE', *, *, #142328, .F. ) ;
#57666=VERTEX_POINT ( 'NONE', #86485 ) ;
#57667=AXIS2_PLACEMENT_3D ( 'NONE', #93996, #72312, #7696 ) ;
#57668=( BOUNDED_CURVE ( )  B_SPLINE_CURVE ( 3, ( #142437, #143131, #30829, #64876 ),
 .UNSPECIFIED., .F., .T. ) 
 B_SPLINE_CURVE_WITH_KNOTS ( ( 4, 4 ),
 ( 1.208578181583236821, 1.359146454359482670 ),
 .UNSPECIFIED. ) 
 CURVE ( )  GEOMETRIC_REPRESENTATION_ITEM ( )  RATIONAL_B_SPLINE_CURVE ( ( 1.000000000000000000, 0.9981116584018941973, 0.9981116584018941973, 1.000000000000000000 ) ) 
 REPRESENTATION_ITEM ( '' )  );
#57669=PLANE ( 'NONE',  #33753 ) ;
#57670=CARTESIAN_POINT ( 'NONE',  ( -15.48921356237309510, -27.52281430457066236, 5.000000000000000000 ) ) ;
#57671=VECTOR ( 'NONE', #138911, 1000.000000000000000 ) ;
#57672=CARTESIAN_POINT ( 'NONE',  ( -13.08316395874281568, 3.014287036135060660, 4.000000000000000000 ) ) ;
#57673=DIRECTION ( 'NONE',  ( 0.3543493200069162685, -0.000000000000000000, -0.9351131265310288487 ) ) ;
#57674=CARTESIAN_POINT ( 'NONE',  ( -20.99999999999984368, -16.02097659208072855, -11.96015758381203575 ) ) ;
#57675=ORIENTED_EDGE ( 'NONE', *, *, #19396, .F. ) ;
#57676=DIRECTION ( 'NONE',  ( -0.6830127018922180770, -0.6830127018922204085, -0.2588190451025213501 ) ) ;
#57677=CARTESIAN_POINT ( 'NONE',  ( 2.229957205422063993, 21.73644205237997440, 5.000000000000000888 ) ) ;
#57678=DIRECTION ( 'NONE',  ( -0.6830127018922180770, -0.6830127018922204085, -0.2588190451025213501 ) ) ;
#57680=CARTESIAN_POINT ( 'NONE',  ( 24.98155265364315625, 18.75929247661553134, 20.33588619593437485 ) ) ;
#57682=EDGE_LOOP ( 'NONE', ( #57612, #125480, #102992, #11630 ) ) ;
#57684=EDGE_LOOP ( 'NONE', ( #37575, #100377, #101307, #28354 ) ) ;
#57687=ORIENTED_EDGE ( 'NONE', *, *, #89116, .T. ) ;
#57689=DIRECTION ( 'NONE',  ( 0.7071067811865486830, -0.7071067811865464625, -0.000000000000000000 ) ) ;
#57690=LINE ( 'NONE', #121476, #94273 ) ;
#57691=CARTESIAN_POINT ( 'NONE',  ( -39.29974487139159578, -27.71228299555233576, 4.000000000000000000 ) ) ;
#57692=CARTESIAN_POINT ( 'NONE',  ( -34.47516574401892342, 4.490517612115571211, 4.998110765256835286 ) ) ;
#57693=VERTEX_POINT ( 'NONE', #53867 ) ;
#57694=ORIENTED_EDGE ( 'NONE', *, *, #95833, .T. ) ;
#57695=VECTOR ( 'NONE', #105347, 1000.000000000000000 ) ;
#57697=VERTEX_POINT ( 'NONE', #19774 ) ;
#57698=DIRECTION ( 'NONE',  ( -0.3543493200069162685, -0.000000000000000000, -0.9351131265310288487 ) ) ;
#57700=CARTESIAN_POINT ( 'NONE',  ( 14.58437909282842426, -0.7858193515946185759, 4.111732654926449015 ) ) ;
#57701=EDGE_LOOP ( 'NONE', ( #8316, #6697, #113915, #95209 ) ) ;
#57702=FACE_BOUND ( 'NONE', #95246, .T. ) ;
#57703=CARTESIAN_POINT ( 'NONE',  ( 69.48921356237309510, -27.52281430457103895, 5.000000000000000000 ) ) ;
#57704=DIRECTION ( 'NONE',  ( -0.7071067811865486830, -0.7071067811865464625, 0.000000000000000000 ) ) ;
#57705=FACE_OUTER_BOUND ( 'NONE', #140407, .T. ) ;
#57706=CARTESIAN_POINT ( 'NONE',  ( 1.499999999999997780, 16.46639925780209168, 5.000000000000000000 ) ) ;
#57709=EDGE_LOOP ( 'NONE', ( #53841, #86131, #36945 ) ) ;
#57710=ORIENTED_EDGE ( 'NONE', *, *, #60946, .T. ) ;
#57712=ORIENTED_EDGE ( 'NONE', *, *, #121698, .F. ) ;
#57713=CARTESIAN_POINT ( 'NONE',  ( -34.92500000000001137, 22.22500000000000142, 4.000000000000000000 ) ) ;
#57714=EDGE_LOOP ( 'NONE', ( #10000, #100511, #87320, #82639 ) ) ;
#57715=CARTESIAN_POINT ( 'NONE',  ( -12.48921356237309155, -27.52281430457064104, 5.000000000000000000 ) ) ;
#57717=SPHERICAL_SURFACE ( 'NONE', #139726, 0.5000000000000000000 ) ;
#57718=EDGE_LOOP ( 'NONE', ( #6158, #36528, #53607, #127436 ) ) ;
#57719=CARTESIAN_POINT ( 'NONE',  ( -0.4892135623730947680, -27.52281430457055578, 5.000000000000000000 ) ) ;
#57721=DIRECTION ( 'NONE',  ( 0.6830127018922180770, -0.6830127018922204085, -0.2588190451025213501 ) ) ;
#57726=AXIS2_PLACEMENT_3D ( 'NONE', #76573, #120752, #66400 ) ;
#57727=VERTEX_POINT ( 'NONE', #11012 ) ;
#57728=DIRECTION ( 'NONE',  ( -0.000000000000000000, -0.000000000000000000, 1.000000000000000000 ) ) ;
#57729=DIRECTION ( 'NONE',  ( -0.000000000000000000, 0.000000000000000000, 1.000000000000000000 ) ) ;
#57730=VECTOR ( 'NONE', #93351, 1000.000000000000000 ) ;
#57732=EDGE_LOOP ( 'NONE', ( #78220, #6063, #130297, #14502 ) ) ;
#57734=EDGE_CURVE ( 'NONE', #29906, #32532, #76317, .T. ) ;
#57735=EDGE_CURVE ( 'NONE', #113850, #5145, #108180, .T. ) ;
#57736=VERTEX_POINT ( 'NONE', #126 ) ;
#57738=ORIENTED_EDGE ( 'NONE', *, *, #80871, .T. ) ;
#57740=EDGE_CURVE ( 'NONE', #80483, #123482, #123412, .T. ) ;
#57741=EDGE_CURVE ( 'NONE', #61260, #82836, #60845, .T. ) ;
#57744=LINE ( 'NONE', #35286, #59070 ) ;
#57745=ORIENTED_EDGE ( 'NONE', *, *, #98847, .T. ) ;
#57747=CARTESIAN_POINT ( 'NONE',  ( -48.18398860626899705, 28.73617430169820608, 5.000000000000000000 ) ) ;
#57748=ORIENTED_EDGE ( 'NONE', *, *, #5526, .F. ) ;
#57749=DIRECTION ( 'NONE',  ( 0.7071067811865486830, -0.7071067811865464625, -0.000000000000000000 ) ) ;
#57750=VECTOR ( 'NONE', #31401, 1000.000000000000227 ) ;
#57752=DIRECTION ( 'NONE',  ( 0.7071067811865486830, -0.7071067811865464625, -0.000000000000000000 ) ) ;
#57753=ORIENTED_EDGE ( 'NONE', *, *, #97046, .T. ) ;
#57755=CARTESIAN_POINT ( 'NONE',  ( 16.40832548098991239, -0.7407075233842701500, 14.76736230305384190 ) ) ;
#57756=LINE ( 'NONE', #70081, #72991 ) ;
#57757=EDGE_CURVE ( 'NONE', #72725, #76924, #93426, .T. ) ;
#57758=ORIENTED_EDGE ( 'NONE', *, *, #51924, .T. ) ;
#57759=VECTOR ( 'NONE', #89363, 999.9999999999998863 ) ;
#57760=DIRECTION ( 'NONE',  ( 0.3543493200069162685, -0.000000000000000000, -0.9351131265310288487 ) ) ;
#57761=VERTEX_POINT ( 'NONE', #72434 ) ;
#57762=EDGE_LOOP ( 'NONE', ( #103894, #56451, #113322, #35903 ) ) ;
#57763=ORIENTED_EDGE ( 'NONE', *, *, #12528, .T. ) ;
#57764=LINE ( 'NONE', #114253, #70227 ) ;
#57765=VECTOR ( 'NONE', #106666, 1000.000000000000000 ) ;
#57766=VECTOR ( 'NONE', #135877, 1000.000000000000000 ) ;
#57768=VECTOR ( 'NONE', #87378, 1000.000000000000000 ) ;
#57769=DIRECTION ( 'NONE',  ( -0.7071067811865486830, -0.7071067811865464625, 0.000000000000000000 ) ) ;
#57770=CARTESIAN_POINT ( 'NONE',  ( -8.999999999999932498, 19.93112307739198386, 4.000000000000000000 ) ) ;
#57771=VECTOR ( 'NONE', #95801, 1000.000000000000227 ) ;
#57773=EDGE_LOOP ( 'NONE', ( #17223, #14109, #95807, #65618 ) ) ;
#57774=AXIS2_PLACEMENT_3D ( 'NONE', #68005, #1239, #122303 ) ;
#57775=EDGE_CURVE ( 'NONE', #11393, #7217, #89323, .T. ) ;
#57777=CARTESIAN_POINT ( 'NONE',  ( 14.90156419391754916, 11.25929247661560595, 10.79108189686410491 ) ) ;
#57779=FACE_OUTER_BOUND ( 'NONE', #26909, .T. ) ;
#57780=LINE ( 'NONE', #91117, #122463 ) ;
#57781=FACE_OUTER_BOUND ( 'NONE', #4400, .T. ) ;
#57782=ORIENTED_EDGE ( 'NONE', *, *, #81474, .F. ) ;
#57784=EDGE_CURVE ( 'NONE', #51247, #115197, #137662, .T. ) ;
#57785=ORIENTED_EDGE ( 'NONE', *, *, #125210, .T. ) ;
#57786=DIRECTION ( 'NONE',  ( 0.7071067811865487940, -0.7071067811865463515, 0.000000000000000000 ) ) ;
#57789=CARTESIAN_POINT ( 'NONE',  ( 60.29974487139158867, -27.71228299555248142, 4.000000000000000000 ) ) ;
#57791=EDGE_CURVE ( 'NONE', #102386, #142915, #45148, .T. ) ;
#57792=DIRECTION ( 'NONE',  ( -0.7071067811865487940, 0.7071067811865463515, 0.000000000000000000 ) ) ;
#57793=CARTESIAN_POINT ( 'NONE',  ( -11.99451991528749417, 28.92564299267946382, 4.000000000000000000 ) ) ;
#57794=DIRECTION ( 'NONE',  ( -0.000000000000000000, 0.000000000000000000, 1.000000000000000000 ) ) ;
#57796=EDGE_CURVE ( 'NONE', #91593, #14375, #39041, .T. ) ;
#57797=FACE_OUTER_BOUND ( 'NONE', #58527, .T. ) ;
#57798=ORIENTED_EDGE ( 'NONE', *, *, #18551, .T. ) ;
#57800=VERTEX_POINT ( 'NONE', #134266 ) ;
#57801=EDGE_CURVE ( 'NONE', #137194, #122494, #57434, .T. ) ;
#57802=CARTESIAN_POINT ( 'NONE',  ( 34.92499999999998295, -0.8020632299005416854, 13.72581505463526064 ) ) ;
#57803=CARTESIAN_POINT ( 'NONE',  ( -3.005480084712505828, 28.92564299267936079, 4.000000000000000000 ) ) ;
#57805=DIRECTION ( 'NONE',  ( 0.3543493200069162685, -0.000000000000000000, -0.9351131265310288487 ) ) ;
#57808=VERTEX_POINT ( 'NONE', #68329 ) ;
#57809=FACE_OUTER_BOUND ( 'NONE', #62, .T. ) ;
#57810=EDGE_LOOP ( 'NONE', ( #12474, #113001, #73723, #106122 ) ) ;
#57811=DIRECTION ( 'NONE',  ( -0.7071067811865487940, 0.7071067811865463515, -0.000000000000000000 ) ) ;
#57812=EDGE_LOOP ( 'NONE', ( #103292, #95682, #130212, #20277 ) ) ;
#57813=ADVANCED_FACE ( 'NONE', ( #15806 ), #112502, .F. ) ;
#57814=DIRECTION ( 'NONE',  ( 0.7071067811865486830, -0.7071067811865464625, -0.000000000000000000 ) ) ;
#57817=VERTEX_POINT ( 'NONE', #49940 ) ;
#57818=EDGE_CURVE ( 'NONE', #40570, #117341, #101619, .T. ) ;
#57820=CARTESIAN_POINT ( 'NONE',  ( 14.81601139373099585, 28.73617430169776910, 5.000000000000000000 ) ) ;
#57823=DIRECTION ( 'NONE',  ( -0.6830127018922181881, 0.6830127018922202975, -0.2588190451025214056 ) ) ;
#57824=DIRECTION ( 'NONE',  ( 0.000000000000000000, 0.000000000000000000, 1.000000000000000000 ) ) ;
#57825=ORIENTED_EDGE ( 'NONE', *, *, #76492, .T. ) ;
#57826=DIRECTION ( 'NONE',  ( -0.6830127018922180770, -0.6830127018922204085, -0.2588190451025213501 ) ) ;
#57827=ORIENTED_EDGE ( 'NONE', *, *, #115787, .T. ) ;
#57828=ADVANCED_FACE ( 'NONE', ( #83267 ), #16554, .F. ) ;
#57830=FACE_OUTER_BOUND ( 'NONE', #73273, .T. ) ;
#57831=CARTESIAN_POINT ( 'NONE',  ( 34.92499999999998295, -3.425372908132426453, 14.71988515618268423 ) ) ;
#57832=FACE_OUTER_BOUND ( 'NONE', #65737, .T. ) ;
#57834=EDGE_LOOP ( 'NONE', ( #471, #68902, #13091, #120973 ) ) ;
#57835=AXIS2_PLACEMENT_3D ( 'NONE', #14745, #92287, #26346 ) ;
#57836=VECTOR ( 'NONE', #125877, 1000.000000000000000 ) ;
#57837=VECTOR ( 'NONE', #77724, 1000.000000000000000 ) ;
#57838=LINE ( 'NONE', #23758, #100750 ) ;
#57839=CARTESIAN_POINT ( 'NONE',  ( -16.17183060077636014, 15.75929247661555443, 4.000000000000000000 ) ) ;
#57840=AXIS2_PLACEMENT_3D ( 'NONE', #38636, #61157, #40096 ) ;
#57841=CARTESIAN_POINT ( 'NONE',  ( -17.28769006033960309, -21.73547319004781642, 4.999917730833662866 ) ) ;
#57842=VERTEX_POINT ( 'NONE', #92691 ) ;
#57843=CARTESIAN_POINT ( 'NONE',  ( 24.64327148205084939, 5.259292476615662792, 4.831541298974423526 ) ) ;
#57844=DIRECTION ( 'NONE',  ( -0.7071067811865486830, -0.7071067811865464625, -0.000000000000000000 ) ) ;
#57845=DIRECTION ( 'NONE',  ( 0.7071067811865486830, -0.7071067811865464625, -0.000000000000000000 ) ) ;
#57846=ORIENTED_EDGE ( 'NONE', *, *, #12121, .F. ) ;
#57847=CARTESIAN_POINT ( 'NONE',  ( -1.001930566820972812, -22.22500000000000142, 4.500000000000000888 ) ) ;
#57848=LINE ( 'NONE', #45549, #56844 ) ;
#57849=FACE_OUTER_BOUND ( 'NONE', #118562, .T. ) ;
#57850=DIRECTION ( 'NONE',  ( -0.3543493200069162685, -0.000000000000000000, -0.9351131265310288487 ) ) ;
#57852=( BOUNDED_CURVE ( )  B_SPLINE_CURVE ( 3, ( #64023, #118377, #53880, #107511 ),
 .UNSPECIFIED., .F., .F. ) 
 B_SPLINE_CURVE_WITH_KNOTS ( ( 4, 4 ),
 ( 5.106027341939276099, 6.645403452391245303 ),
 .UNSPECIFIED. ) 
 CURVE ( )  GEOMETRIC_REPRESENTATION_ITEM ( )  RATIONAL_B_SPLINE_CURVE ( ( 1.000000000000000000, 0.8120851936182269526, 0.8120851936182269526, 1.000000000000000000 ) ) 
 REPRESENTATION_ITEM ( '' )  );
#57853=DIRECTION ( 'NONE',  ( -0.000000000000000000, 0.3543493200069153248, 0.9351131265310292928 ) ) ;
#57854=ORIENTED_EDGE ( 'NONE', *, *, #84921, .T. ) ;
#57855=EDGE_CURVE ( 'NONE', #98898, #138457, #136927, .T. ) ;
#57856=ORIENTED_EDGE ( 'NONE', *, *, #34253, .F. ) ;
#57857=VERTEX_POINT ( 'NONE', #94118 ) ;
#57859=AXIS2_PLACEMENT_3D ( 'NONE', #2822, #136916, #36875 ) ;
#57860=ORIENTED_EDGE ( 'NONE', *, *, #53949, .T. ) ;
#57861=DIRECTION ( 'NONE',  ( 0.7071067811865486830, -0.7071067811865464625, -0.000000000000000000 ) ) ;
#57862=DIRECTION ( 'NONE',  ( 0.7071067811865487940, 0.7071067811865463515, 0.000000000000000000 ) ) ;
#57863=VECTOR ( 'NONE', #133575, 999.9999999999998863 ) ;
#57865=LINE ( 'NONE', #68049, #80204 ) ;
#57866=ORIENTED_EDGE ( 'NONE', *, *, #111919, .T. ) ;
#57868=DIRECTION ( 'NONE',  ( -0.6830127018922180770, -0.6830127018922204085, -0.2588190451025213501 ) ) ;
#57869=LINE ( 'NONE', #69446, #18653 ) ;
#57870=VECTOR ( 'NONE', #121458, 1000.000000000000000 ) ;
#57872=EDGE_CURVE ( 'NONE', #16056, #78330, #34968, .T. ) ;
#57874=DIRECTION ( 'NONE',  ( -0.7071067811865486830, -0.7071067811865464625, -0.000000000000000000 ) ) ;
#57875=DIRECTION ( 'NONE',  ( -0.7071067811865487940, 0.7071067811865463515, 0.000000000000000000 ) ) ;
#57876=VECTOR ( 'NONE', #135232, 1000.000000000000000 ) ;
#57877=VECTOR ( 'NONE', #115690, 1000.000000000000000 ) ;
#57878=ORIENTED_EDGE ( 'NONE', *, *, #26850, .T. ) ;
#57879=VERTEX_POINT ( 'NONE', #138359 ) ;
#57880=FACE_OUTER_BOUND ( 'NONE', #117268, .T. ) ;
#57881=EDGE_CURVE ( 'NONE', #97802, #73980, #2271, .T. ) ;
#57882=VECTOR ( 'NONE', #82002, 1000.000000000000000 ) ;
#57883=CARTESIAN_POINT ( 'NONE',  ( -42.29974487139158157, -27.71228299555235708, 4.000000000000000000 ) ) ;
#57886=VECTOR ( 'NONE', #25698, 1000.000000000000000 ) ;
#57887=CARTESIAN_POINT ( 'NONE',  ( -63.48921356237309510, -27.52281430457099631, 5.000000000000000000 ) ) ;
#57888=DIRECTION ( 'NONE',  ( 1.000000000000000000, 0.000000000000000000, 0.000000000000000000 ) ) ;
#57891=ORIENTED_EDGE ( 'NONE', *, *, #134438, .T. ) ;
#57892=ORIENTED_EDGE ( 'NONE', *, *, #36686, .T. ) ;
#57893=DIRECTION ( 'NONE',  ( 0.7071067811865487940, -0.7071067811865463515, 0.000000000000000000 ) ) ;
#57894=ORIENTED_EDGE ( 'NONE', *, *, #81051, .F. ) ;
#57896=VECTOR ( 'NONE', #43889, 999.9999999999998863 ) ;
#57897=PLANE ( 'NONE',  #105240 ) ;
#57898=ORIENTED_EDGE ( 'NONE', *, *, #59981, .T. ) ;
#57900=LINE ( 'NONE', #45598, #125890 ) ;
#57901=EDGE_CURVE ( 'NONE', #71697, #106502, #11731, .T. ) ;
#57902=DIRECTION ( 'NONE',  ( -0.7071067811865487940, 0.7071067811865463515, 0.000000000000000000 ) ) ;
#57903=CARTESIAN_POINT ( 'NONE',  ( -35.01844734635648138, 18.75929247661553134, 20.33588619593451341 ) ) ;
#57904=EDGE_CURVE ( 'NONE', #81604, #105391, #34238, .T. ) ;
#57905=VECTOR ( 'NONE', #15422, 1000.000000000000227 ) ;
#57906=PLANE ( 'NONE',  #111641 ) ;
#57907=ORIENTED_EDGE ( 'NONE', *, *, #135394, .F. ) ;
#57908=CARTESIAN_POINT ( 'NONE',  ( -13.49999999999990408, -19.53360074219754594, 5.000000000000000000 ) ) ;
#57910=ORIENTED_EDGE ( 'NONE', *, *, #45438, .F. ) ;
#57913=CARTESIAN_POINT ( 'NONE',  ( -24.29974487139158867, -27.71228299555223273, 4.000000000000000000 ) ) ;
#57914=EDGE_CURVE ( 'NONE', #45084, #137138, #111795, .T. ) ;
#57915=EDGE_LOOP ( 'NONE', ( #21536, #84690, #138665, #82397 ) ) ;
#57916=EDGE_CURVE ( 'NONE', #29477, #90522, #82824, .T. ) ;
#57917=LINE ( 'NONE', #92624, #96792 ) ;
#57918=EDGE_LOOP ( 'NONE', ( #50201, #38300, #120216, #7663 ) ) ;
#57919=ORIENTED_EDGE ( 'NONE', *, *, #128156, .T. ) ;
#57920=VERTEX_POINT ( 'NONE', #50633 ) ;
#57922=ADVANCED_FACE ( 'NONE', ( #84013 ), #107143, .F. ) ;
#57924=CARTESIAN_POINT ( 'NONE',  ( -63.18398860626900415, 28.73617430169831621, 5.000000000000000000 ) ) ;
#57925=LINE ( 'NONE', #138306, #10315 ) ;
#57926=EDGE_CURVE ( 'NONE', #133007, #84626, #130352, .T. ) ;
#57928=PLANE ( 'NONE',  #51794 ) ;
#57929=EDGE_CURVE ( 'NONE', #29579, #48649, #81983, .T. ) ;
#57930=DIRECTION ( 'NONE',  ( -0.000000000000000000, 0.3543493200069153248, 0.9351131265310292928 ) ) ;
#57931=CARTESIAN_POINT ( 'NONE',  ( -17.56319896779159606, -12.74070752338415069, 9.898150129686415610 ) ) ;
#57932=EDGE_CURVE ( 'NONE', #108166, #83276, #9216, .T. ) ;
#57933=CYLINDRICAL_SURFACE ( 'NONE', #77101, 0.5000000000000004441 ) ;
#57934=CARTESIAN_POINT ( 'NONE',  ( -12.29974487139158512, -27.71228299555214747, 4.000000000000000000 ) ) ;
#57935=EDGE_CURVE ( 'NONE', #59881, #5654, #117987, .T. ) ;
#57936=VECTOR ( 'NONE', #105665, 1000.000000000000000 ) ;
#57937=ORIENTED_EDGE ( 'NONE', *, *, #14852, .F. ) ;
#57940=ORIENTED_EDGE ( 'NONE', *, *, #35845, .F. ) ;
#57941=VECTOR ( 'NONE', #95263, 1000.000000000000000 ) ;
#57942=LINE ( 'NONE', #92650, #19442 ) ;
#57943=AXIS2_PLACEMENT_3D ( 'NONE', #40107, #140115, #6675 ) ;
#57944=AXIS2_PLACEMENT_3D ( 'NONE', #30494, #129069, #128379 ) ;
#57945=VERTEX_POINT ( 'NONE', #107838 ) ;
#57946=VECTOR ( 'NONE', #23117, 1000.000000000000000 ) ;
#57947=AXIS2_PLACEMENT_3D ( 'NONE', #108847, #131349, #97247 ) ;
#57948=CARTESIAN_POINT ( 'NONE',  ( -18.18398860626898994, 28.73617430169800002, 5.000000000000000000 ) ) ;
#57950=EDGE_CURVE ( 'NONE', #94597, #74021, #62240, .T. ) ;
#57951=CARTESIAN_POINT ( 'NONE',  ( -24.70710678118637205, 20.25929247661551713, 5.000000000000000000 ) ) ;
#57952=CARTESIAN_POINT ( 'NONE',  ( -19.49999999999987210, -2.777013188829482893, 4.549262955118030582 ) ) ;
#57954=LINE ( 'NONE', #59373, #88201 ) ;
#57955=VERTEX_POINT ( 'NONE', #106396 ) ;
#57956=EDGE_CURVE ( 'NONE', #18457, #97230, #141955, .T. ) ;
#57957=DIRECTION ( 'NONE',  ( -0.6830127018922181881, 0.6830127018922202975, -0.2588190451025214056 ) ) ;
#57959=ORIENTED_EDGE ( 'NONE', *, *, #19772, .F. ) ;
#57960=CARTESIAN_POINT ( 'NONE',  ( 42.48921356237308800, -27.52281430457085065, 5.000000000000000000 ) ) ;
#57961=CARTESIAN_POINT ( 'NONE',  ( -2.510786437626908008, -27.52281430457053446, 5.000000000000000000 ) ) ;
#57962=ORIENTED_EDGE ( 'NONE', *, *, #51502, .F. ) ;
#57963=VERTEX_POINT ( 'NONE', #131054 ) ;
#57964=VERTEX_POINT ( 'NONE', #52066 ) ;
#57965=DIRECTION ( 'NONE',  ( 1.000000000000000000, 0.000000000000000000, 0.000000000000000000 ) ) ;
#57967=DIRECTION ( 'NONE',  ( 0.7071067811865487940, -0.7071067811865463515, 0.000000000000000000 ) ) ;
#57968=DIRECTION ( 'NONE',  ( -0.000000000000000000, -0.3543493200069152693, 0.9351131265310292928 ) ) ;
#57969=LINE ( 'NONE', #102166, #17246 ) ;
#57970=EDGE_LOOP ( 'NONE', ( #79672, #91231, #5868, #59714 ) ) ;
#57971=FACE_OUTER_BOUND ( 'NONE', #42832, .T. ) ;
#57972=CARTESIAN_POINT ( 'NONE',  ( -13.10966639810773771, 3.759292476615678336, 4.164048746910666843 ) ) ;
#57974=CARTESIAN_POINT ( 'NONE',  ( -0.2997448713915885632, -27.71228299555206220, 4.000000000000000000 ) ) ;
#57975=LINE ( 'NONE', #15800, #95422 ) ;
#57976=EDGE_CURVE ( 'NONE', #66483, #30242, #39787, .T. ) ;
#57977=VECTOR ( 'NONE', #69964, 999.9999999999998863 ) ;
#57978=ORIENTED_EDGE ( 'NONE', *, *, #136480, .T. ) ;
#57979=CARTESIAN_POINT ( 'NONE',  ( -19.49999999999986144, -16.91253812416058366, 4.000000000000000000 ) ) ;
#57982=EDGE_CURVE ( 'NONE', #43201, #93841, #96945, .T. ) ;
#57983=CARTESIAN_POINT ( 'NONE',  ( -16.49999999999988276, -15.29013452822855967, 0.3645803511609976288 ) ) ;
#57984=VERTEX_POINT ( 'NONE', #19427 ) ;
#57986=VECTOR ( 'NONE', #6183, 1000.000000000000000 ) ;
#57987=LINE ( 'NONE', #102181, #5348 ) ;
#57988=DIRECTION ( 'NONE',  ( 1.000000000000000000, 0.000000000000000000, 0.000000000000000000 ) ) ;
#57989=VERTEX_POINT ( 'NONE', #96241 ) ;
#57991=VERTEX_POINT ( 'NONE', #29577 ) ;
#57992=ADVANCED_FACE ( 'NONE', ( #30306 ), #116601, .F. ) ;
#57993=CARTESIAN_POINT ( 'NONE',  ( 34.92499999999998295, -8.028593703617110222, -6.464217593021339248 ) ) ;
#57994=CARTESIAN_POINT ( 'NONE',  ( -57.29974487139158157, -27.71228299555246011, 4.000000000000000000 ) ) ;
#57995=CARTESIAN_POINT ( 'NONE',  ( 2.999999999999978240, 4.965500833774331824, -4.007596771432663907 ) ) ;
#57996=DIRECTION ( 'NONE',  ( -0.000000000000000000, -0.3543493200069152693, 0.9351131265310292928 ) ) ;
#57997=FACE_OUTER_BOUND ( 'NONE', #8952, .T. ) ;
#57999=PLANE ( 'NONE',  #102374 ) ;
#58000=LINE ( 'NONE', #3542, #86486 ) ;
#58001=CARTESIAN_POINT ( 'NONE',  ( 12.18398860626900060, 28.73617430169795739, 5.000000000000000000 ) ) ;
#58003=VECTOR ( 'NONE', #84382, 999.9999999999998863 ) ;
#58005=LINE ( 'NONE', #34799, #92178 ) ;
#58006=CARTESIAN_POINT ( 'NONE',  ( 26.51078643762690845, -27.52281430457036748, 5.000000000000000000 ) ) ;
#58007=DIRECTION ( 'NONE',  ( -0.000000000000000000, -0.3543493200069152693, 0.9351131265310292928 ) ) ;
#58008=VERTEX_POINT ( 'NONE', #41174 ) ;
#58009=ORIENTED_EDGE ( 'NONE', *, *, #25324, .T. ) ;
#58011=ORIENTED_EDGE ( 'NONE', *, *, #59723, .F. ) ;
#58012=VERTEX_POINT ( 'NONE', #139083 ) ;
#58013=ORIENTED_EDGE ( 'NONE', *, *, #142669, .T. ) ;
#58014=CARTESIAN_POINT ( 'NONE',  ( 51.48921356237309510, -27.52281430457091460, 5.000000000000000000 ) ) ;
#58015=DIRECTION ( 'NONE',  ( 0.7071067811865486830, -0.7071067811865464625, -0.000000000000000000 ) ) ;
#58016=VECTOR ( 'NONE', #77551, 1000.000000000000000 ) ;
#58020=CARTESIAN_POINT ( 'NONE',  ( -69.18398860626899705, 28.73617430169835529, 5.000000000000000000 ) ) ;
#58021=FACE_OUTER_BOUND ( 'NONE', #624, .T. ) ;
#58023=EDGE_CURVE ( 'NONE', #86178, #138040, #85384, .T. ) ;
#58024=EDGE_CURVE ( 'NONE', #120984, #106637, #1218, .T. ) ;
#58026=CARTESIAN_POINT ( 'NONE',  ( 5.206660635421493488, 21.75929247661549937, 4.998822639870701856 ) ) ;
#58027=LINE ( 'NONE', #71027, #116778 ) ;
#58028=CARTESIAN_POINT ( 'NONE',  ( -4.499999999999967137, 6.052185695429111334, 5.000000000000000000 ) ) ;
#58030=AXIS2_PLACEMENT_3D ( 'NONE', #106979, #19967, #7661 ) ;
#58031=CARTESIAN_POINT ( 'NONE',  ( 15.48921356237309510, -27.52281430457066236, 5.000000000000000000 ) ) ;
#58032=DIRECTION ( 'NONE',  ( -0.7071067811865487940, 0.7071067811865463515, 0.000000000000000000 ) ) ;
#58033=DIRECTION ( 'NONE',  ( 0.7071067811865487940, 0.7071067811865463515, 0.000000000000000000 ) ) ;
#58035=VERTEX_POINT ( 'NONE', #75957 ) ;
#58036=VERTEX_POINT ( 'NONE', #22959 ) ;
#58038=EDGE_LOOP ( 'NONE', ( #26679, #84699, #115724, #91926 ) ) ;
#58039=EDGE_CURVE ( 'NONE', #42167, #39995, #43335, .T. ) ;
#58040=DIRECTION ( 'NONE',  ( -0.6830127018922180770, -0.6830127018922202975, -0.2588190451025213501 ) ) ;
#58041=DIRECTION ( 'NONE',  ( 0.7071067811865487940, 0.7071067811865463515, 0.000000000000000000 ) ) ;
#58042=VECTOR ( 'NONE', #45333, 999.9999999999998863 ) ;
#58043=CARTESIAN_POINT ( 'NONE',  ( 8.510786437626906675, -27.52281430457049183, 5.000000000000000000 ) ) ;
#58044=CARTESIAN_POINT ( 'NONE',  ( 30.48921356237309510, -27.52281430457076894, 5.000000000000000000 ) ) ;
#58045=EDGE_CURVE ( 'NONE', #83916, #40909, #101604, .T. ) ;
#58046=VECTOR ( 'NONE', #112265, 1000.000000000000227 ) ;
#58050=EDGE_LOOP ( 'NONE', ( #100888, #127988, #51324, #77807 ) ) ;
#58053=AXIS2_PLACEMENT_3D ( 'NONE', #60811, #27397, #14406 ) ;
#58056=AXIS2_PLACEMENT_3D ( 'NONE', #3080, #103798, #60354 ) ;
#58058=VECTOR ( 'NONE', #57749, 1000.000000000000000 ) ;
#58059=ORIENTED_EDGE ( 'NONE', *, *, #134001, .T. ) ;
#58062=CARTESIAN_POINT ( 'NONE',  ( 33.66846741159835688, -18.74070752338409562, 20.73178291233849535 ) ) ;
#58063=ADVANCED_FACE ( 'NONE', ( #32462 ), #76699, .F. ) ;
#58064=DIRECTION ( 'NONE',  ( -0.7071067811865487940, 0.7071067811865463515, 0.000000000000000000 ) ) ;
#58065=VECTOR ( 'NONE', #34816, 1000.000000000000227 ) ;
#58067=ORIENTED_EDGE ( 'NONE', *, *, #133808, .T. ) ;
#58068=VERTEX_POINT ( 'NONE', #90397 ) ;
#58070=VERTEX_POINT ( 'NONE', #67984 ) ;
#58071=VERTEX_POINT ( 'NONE', #56393 ) ;
#58072=VECTOR ( 'NONE', #40330, 999.9999999999998863 ) ;
#58074=DIRECTION ( 'NONE',  ( -1.000000000000000000, -1.424048422229243832E-14, 0.000000000000000000 ) ) ;
#58075=VECTOR ( 'NONE', #112938, 1000.000000000000227 ) ;
#58076=DIRECTION ( 'NONE',  ( 0.7071067811865486830, -0.7071067811865464625, -0.000000000000000000 ) ) ;
#58078=ORIENTED_EDGE ( 'NONE', *, *, #91449, .F. ) ;
#58079=LINE ( 'NONE', #35614, #113149 ) ;
#58080=AXIS2_PLACEMENT_3D ( 'NONE', #104675, #138031, #17646 ) ;
#58081=LINE ( 'NONE', #137028, #43736 ) ;
#58082=AXIS2_PLACEMENT_3D ( 'NONE', #122852, #22092, #66349 ) ;
#58084=FACE_BOUND ( 'NONE', #46881, .T. ) ;
#58085=ORIENTED_EDGE ( 'NONE', *, *, #10098, .F. ) ;
#58087=DIRECTION ( 'NONE',  ( -0.7071067811865487940, 0.7071067811865463515, 0.000000000000000000 ) ) ;
#58090=ORIENTED_EDGE ( 'NONE', *, *, #41484, .T. ) ;
#58091=DIRECTION ( 'NONE',  ( -0.3543493200069162685, -0.000000000000000000, -0.9351131265310288487 ) ) ;
#58092=ORIENTED_EDGE ( 'NONE', *, *, #11433, .F. ) ;
#58093=ORIENTED_EDGE ( 'NONE', *, *, #46361, .T. ) ;
#58094=ORIENTED_EDGE ( 'NONE', *, *, #63248, .T. ) ;
#58095=EDGE_CURVE ( 'NONE', #8673, #37784, #10663, .T. ) ;
#58097=ORIENTED_EDGE ( 'NONE', *, *, #71820, .T. ) ;
#58099=CARTESIAN_POINT ( 'NONE',  ( -11.29289321881337571, -6.740707523384214639, 5.000000000000000000 ) ) ;
#58100=EDGE_CURVE ( 'NONE', #113825, #11807, #111425, .T. ) ;
#58102=DIRECTION ( 'NONE',  ( -0.3543493200069162685, -0.000000000000000000, -0.9351131265310288487 ) ) ;
#58103=ORIENTED_EDGE ( 'NONE', *, *, #105231, .F. ) ;
#58104=ADVANCED_FACE ( 'NONE', ( #44053 ), #55644, .T. ) ;
#58106=VECTOR ( 'NONE', #69603, 1000.000000000000227 ) ;
#58107=CARTESIAN_POINT ( 'NONE',  ( -3.489213562373097322, -27.52281430457057709, 5.000000000000000000 ) ) ;
#58108=EDGE_CURVE ( 'NONE', #51759, #133266, #110684, .T. ) ;
#58109=LINE ( 'NONE', #102306, #125622 ) ;
#58111=DIRECTION ( 'NONE',  ( -0.7071067811865486830, -0.7071067811865464625, -0.000000000000000000 ) ) ;
#58112=DIRECTION ( 'NONE',  ( 1.000000000000000000, 0.000000000000000000, 0.000000000000000000 ) ) ;
#58113=ADVANCED_FACE ( 'NONE', ( #9975 ), #142642, .F. ) ;
#58114=VERTEX_POINT ( 'NONE', #122288 ) ;
#58115=ORIENTED_EDGE ( 'NONE', *, *, #100127, .F. ) ;
#58117=VECTOR ( 'NONE', #4170, 1000.000000000000000 ) ;
#58118=ORIENTED_EDGE ( 'NONE', *, *, #44662, .F. ) ;
#58120=ORIENTED_EDGE ( 'NONE', *, *, #74114, .T. ) ;
#58122=DIRECTION ( 'NONE',  ( -0.7071067811865486830, 0.7071067811865464625, 0.000000000000000000 ) ) ;
#58123=ADVANCED_FACE ( 'NONE', ( #99846 ), #66518, .F. ) ;
#58124=EDGE_CURVE ( 'NONE', #67219, #19842, #78109, .T. ) ;
#58125=FACE_OUTER_BOUND ( 'NONE', #32340, .T. ) ;
#58126=EDGE_LOOP ( 'NONE', ( #139207, #7779, #129173, #142091, #103305 ) ) ;
#58128=AXIS2_PLACEMENT_3D ( 'NONE', #85060, #74935, #31409 ) ;
#58130=VERTEX_POINT ( 'NONE', #15642 ) ;
#58131=EDGE_CURVE ( 'NONE', #123040, #46717, #114961, .T. ) ;
#58132=DIRECTION ( 'NONE',  ( -0.7071067811865486830, -0.7071067811865464625, 0.000000000000000000 ) ) ;
#58135=ORIENTED_EDGE ( 'NONE', *, *, #32609, .T. ) ;
#58137=CARTESIAN_POINT ( 'NONE',  ( -22.49999999999984368, -13.91253812416060853, 4.000000000000000000 ) ) ;
#58138=CARTESIAN_POINT ( 'NONE',  ( -21.29974487139158512, -27.71228299555221142, 4.000000000000000000 ) ) ;
#58141=DIRECTION ( 'NONE',  ( -0.6830127018922180770, -0.6830127018922204085, -0.2588190451025213501 ) ) ;
#58143=DIRECTION ( 'NONE',  ( -0.000000000000000000, 0.000000000000000000, 1.000000000000000000 ) ) ;
#58144=CARTESIAN_POINT ( 'NONE',  ( 3.469446951953614189E-15, 10.55218569542906870, 5.000000000000000000 ) ) ;
#58146=AXIS2_PLACEMENT_3D ( 'NONE', #63820, #107984, #8655 ) ;
#58147=CARTESIAN_POINT ( 'NONE',  ( 23.99999999999983302, 18.08204922493375122, 0.9627537363044317287 ) ) ;
#58148=CARTESIAN_POINT ( 'NONE',  ( 42.18398860626899705, 28.73617430169816700, 5.000000000000000000 ) ) ;
#58149=ORIENTED_EDGE ( 'NONE', *, *, #69714, .T. ) ;
#58150=VECTOR ( 'NONE', #136681, 1000.000000000000000 ) ;
#58152=VECTOR ( 'NONE', #139366, 1000.000000000000000 ) ;
#58153=CARTESIAN_POINT ( 'NONE',  ( 29.99999999999979039, 2.342191155542475034, -5.001666872980155887 ) ) ;
#58154=PLANE ( 'NONE',  #127739 ) ;
#58155=EDGE_CURVE ( 'NONE', #10046, #118345, #104840, .T. ) ;
#58158=VECTOR ( 'NONE', #102352, 1000.000000000000000 ) ;
#58159=VECTOR ( 'NONE', #71347, 1000.000000000000000 ) ;
#58161=VECTOR ( 'NONE', #28415, 1000.000000000000000 ) ;
#58162=LINE ( 'NONE', #136376, #70148 ) ;
#58163=VECTOR ( 'NONE', #14021, 1000.000000000000000 ) ;
#58164=ORIENTED_EDGE ( 'NONE', *, *, #99694, .T. ) ;
#58165=DIRECTION ( 'NONE',  ( -0.3543493200069163240, -0.000000000000000000, -0.9351131265310288487 ) ) ;
#58167=ORIENTED_EDGE ( 'NONE', *, *, #101746, .F. ) ;
#58168=CARTESIAN_POINT ( 'NONE',  ( -28.49999999999980105, -17.94781430457063820, 5.000000000000000000 ) ) ;
#58171=VERTEX_POINT ( 'NONE', #25123 ) ;
#58172=CARTESIAN_POINT ( 'NONE',  ( 34.42499999999998295, 19.54139925780185294, 5.000000000000000000 ) ) ;
#58174=VERTEX_POINT ( 'NONE', #101992 ) ;
#58176=CARTESIAN_POINT ( 'NONE',  ( 16.88982677111777875, -22.22500000000000497, 4.785647885939349422 ) ) ;
#58177=EDGE_CURVE ( 'NONE', #113634, #687, #37464, .T. ) ;
#58178=LINE ( 'NONE', #35706, #60584 ) ;
#58181=LINE ( 'NONE', #102373, #51663 ) ;
#58182=DIRECTION ( 'NONE',  ( -0.000000000000000000, 0.000000000000000000, 1.000000000000000000 ) ) ;
#58184=CARTESIAN_POINT ( 'NONE',  ( -21.48921356237309155, -27.52281430457070499, 5.000000000000000000 ) ) ;
#58185=EDGE_LOOP ( 'NONE', ( #131735, #81056, #140542, #20912 ) ) ;
#58187=VERTEX_POINT ( 'NONE', #126574 ) ;
#58188=ORIENTED_EDGE ( 'NONE', *, *, #112245, .T. ) ;
#58190=VECTOR ( 'NONE', #46823, 1000.000000000000000 ) ;
#58191=EDGE_LOOP ( 'NONE', ( #89156, #110377, #107252 ) ) ;
#58192=EDGE_LOOP ( 'NONE', ( #84719, #105484, #102943, #20265 ) ) ;
#58193=EDGE_CURVE ( 'NONE', #107560, #26065, #104097, .T. ) ;
#58195=ORIENTED_EDGE ( 'NONE', *, *, #98134, .T. ) ;
#58196=DIRECTION ( 'NONE',  ( 0.7071067811865486830, -0.7071067811865464625, -0.000000000000000000 ) ) ;
#58197=CARTESIAN_POINT ( 'NONE',  ( 23.99999999999984013, 20.58746187583902909, 4.000000000000000000 ) ) ;
#58198=AXIS2_PLACEMENT_3D ( 'NONE', #33560, #2280, #77061 ) ;
#58199=EDGE_LOOP ( 'NONE', ( #74397, #110668, #65511, #8879 ) ) ;
#58200=CARTESIAN_POINT ( 'NONE',  ( 34.92499999999998295, 22.22500000000000142, 4.500000000000000888 ) ) ;
#58201=DIRECTION ( 'NONE',  ( -0.7071067811865486830, 0.7071067811865464625, 0.000000000000000000 ) ) ;
#58202=CARTESIAN_POINT ( 'NONE',  ( -5.700255128608413102, -27.71228299555201957, 4.000000000000000000 ) ) ;
#58206=AXIS2_PLACEMENT_3D ( 'NONE', #17466, #49429, #104472 ) ;
#58207=ORIENTED_EDGE ( 'NONE', *, *, #22225, .F. ) ;
#58208=CARTESIAN_POINT ( 'NONE',  ( 9.291777089830421943, -15.74070752338411694, 19.73771281079099893 ) ) ;
#58210=CARTESIAN_POINT ( 'NONE',  ( 34.92499999999998295, -2.781974347153350902, -4.476077389926498284 ) ) ;
#58212=PLANE ( 'NONE',  #121533 ) ;
#58213=LINE ( 'NONE', #80642, #120985 ) ;
#58214=CARTESIAN_POINT ( 'NONE',  ( -34.42500000000001137, 4.541399257801965739, 5.000000000000000000 ) ) ;
#58216=LINE ( 'NONE', #114663, #2763 ) ;
#58217=DIRECTION ( 'NONE',  ( -0.000000000000000000, 0.000000000000000000, 1.000000000000000000 ) ) ;
#58218=VECTOR ( 'NONE', #71594, 1000.000000000000000 ) ;
#58219=VERTEX_POINT ( 'NONE', #70127 ) ;
#58220=ORIENTED_EDGE ( 'NONE', *, *, #74311, .F. ) ;
#58222=VERTEX_POINT ( 'NONE', #4759 ) ;
#58224=VECTOR ( 'NONE', #107010, 1000.000000000000000 ) ;
#58225=DIRECTION ( 'NONE',  ( -0.7071067811865487940, 0.7071067811865463515, 0.000000000000000000 ) ) ;
#58227=ORIENTED_EDGE ( 'NONE', *, *, #61710, .F. ) ;
#58228=VECTOR ( 'NONE', #8498, 1000.000000000000000 ) ;
#58229=CARTESIAN_POINT ( 'NONE',  ( 54.18398860626899705, 28.73617430169825226, 5.000000000000000000 ) ) ;
#58230=DIRECTION ( 'NONE',  ( 1.000000000000000000, 0.000000000000000000, 0.000000000000000000 ) ) ;
#58232=EDGE_CURVE ( 'NONE', #139414, #99498, #59241, .T. ) ;
#58234=AXIS2_PLACEMENT_3D ( 'NONE', #48190, #125767, #93124 ) ;
#58235=CARTESIAN_POINT ( 'NONE',  ( 7.630678725896657077, 22.22500000000000142, -11.12593748405039662 ) ) ;
#58237=AXIS2_PLACEMENT_3D ( 'NONE', #138532, #114613, #81313 ) ;
#58238=DIRECTION ( 'NONE',  ( -0.6830127018922180770, -0.6830127018922204085, -0.2588190451025213501 ) ) ;
#58239=LINE ( 'NONE', #90839, #36122 ) ;
#58240=FACE_OUTER_BOUND ( 'NONE', #93557, .T. ) ;
#58241=PLANE ( 'NONE',  #118116 ) ;
#58242=ORIENTED_EDGE ( 'NONE', *, *, #104423, .F. ) ;
#58244=VERTEX_POINT ( 'NONE', #114287 ) ;
#58245=LINE ( 'NONE', #1624, #88754 ) ;
#58246=EDGE_CURVE ( 'NONE', #39048, #75609, #125171, .T. ) ;
#58247=LINE ( 'NONE', #3088, #85550 ) ;
#58248=DIRECTION ( 'NONE',  ( -0.7071067811865486830, -0.7071067811865464625, 0.000000000000000000 ) ) ;
#58249=CARTESIAN_POINT ( 'NONE',  ( 3.489213562373097322, -27.52281430457057709, 5.000000000000000000 ) ) ;
#58252=( BOUNDED_CURVE ( )  B_SPLINE_CURVE ( 3, ( #41851, #96896, #74499, #66472 ),
 .UNSPECIFIED., .F., .T. ) 
 B_SPLINE_CURVE_WITH_KNOTS ( ( 4, 4 ),
 ( 2.431655599645419663, 2.488862747797044861 ),
 .UNSPECIFIED. ) 
 CURVE ( )  GEOMETRIC_REPRESENTATION_ITEM ( )  RATIONAL_B_SPLINE_CURVE ( ( 1.000000000000000000, 0.9997272971104411710, 0.9997272971104411710, 1.000000000000000000 ) ) 
 REPRESENTATION_ITEM ( '' )  );
#58255=CARTESIAN_POINT ( 'NONE',  ( 7.499999999999954703, 10.46639925780215563, 5.000000000000000000 ) ) ;
#58256=ORIENTED_EDGE ( 'NONE', *, *, #127392, .T. ) ;
#58257=EDGE_LOOP ( 'NONE', ( #102322, #140003, #18471, #130513 ) ) ;
#58258=DIRECTION ( 'NONE',  ( 0.7071067811865487940, 0.7071067811865463515, 0.000000000000000000 ) ) ;
#58259=VECTOR ( 'NONE', #16349, 999.9999999999998863 ) ;
#58260=ORIENTED_EDGE ( 'NONE', *, *, #107276, .T. ) ;
#58261=EDGE_CURVE ( 'NONE', #4040, #6529, #14960, .T. ) ;
#58262=VECTOR ( 'NONE', #17734, 999.9999999999998863 ) ;
#58265=ORIENTED_EDGE ( 'NONE', *, *, #115932, .F. ) ;
#58266=DIRECTION ( 'NONE',  ( 0.7071067811865486830, -0.7071067811865464625, -0.000000000000000000 ) ) ;
#58267=VECTOR ( 'NONE', #42086, 1000.000000000000000 ) ;
#58268=VECTOR ( 'NONE', #87574, 1000.000000000000114 ) ;
#58269=DIRECTION ( 'NONE',  ( 0.7071067811865487940, 0.7071067811865463515, -0.000000000000000000 ) ) ;
#58270=VECTOR ( 'NONE', #109475, 1000.000000000000000 ) ;
#58271=VECTOR ( 'NONE', #99908, 1000.000000000000000 ) ;
#58273=CARTESIAN_POINT ( 'NONE',  ( 4.045157733366646191, -21.74070752338405299, 21.72585301388584966 ) ) ;
#58274=FACE_BOUND ( 'NONE', #53371, .T. ) ;
#58275=LINE ( 'NONE', #56114, #101146 ) ;
#58276=DIRECTION ( 'NONE',  ( 1.000000000000000000, 0.000000000000000000, 0.000000000000000000 ) ) ;
#58277=FACE_OUTER_BOUND ( 'NONE', #142843, .T. ) ;
#58278=CARTESIAN_POINT ( 'NONE',  ( -9.183988606268997046, 28.73617430169793607, 5.000000000000000000 ) ) ;
#58279=EDGE_LOOP ( 'NONE', ( #35800, #142777, #102581, #88949 ) ) ;
#58280=ORIENTED_EDGE ( 'NONE', *, *, #105148, .F. ) ;
#58281=FACE_OUTER_BOUND ( 'NONE', #42894, .T. ) ;
#58282=EDGE_LOOP ( 'NONE', ( #49306, #13625, #16512, #142394 ) ) ;
#58283=ADVANCED_FACE ( 'NONE', ( #24424 ), #137487, .F. ) ;
#58284=ORIENTED_EDGE ( 'NONE', *, *, #68063, .F. ) ;
#58288=DIRECTION ( 'NONE',  ( -0.7071067811865487940, 0.7071067811865463515, 0.000000000000000000 ) ) ;
#58289=EDGE_CURVE ( 'NONE', #133168, #11390, #115676, .T. ) ;
#58290=ORIENTED_EDGE ( 'NONE', *, *, #56657, .F. ) ;
#58291=LINE ( 'NONE', #93005, #30541 ) ;
#58292=ADVANCED_FACE ( 'NONE', ( #91141 ), #5506, .F. ) ;
#58293=ADVANCED_FACE ( 'NONE', ( #14262 ), #112853, .F. ) ;
#58294=VECTOR ( 'NONE', #138462, 1000.000000000000000 ) ;
#58295=CARTESIAN_POINT ( 'NONE',  ( 18.29974487139159223, -27.71228299555219010, 4.000000000000000000 ) ) ;
#58297=CARTESIAN_POINT ( 'NONE',  ( 33.48921356237309510, -27.52281430457078670, 5.000000000000000000 ) ) ;
#58298=CARTESIAN_POINT ( 'NONE',  ( 0.000000000000000000, 0.000000000000000000, 5.000000000000000000 ) ) ;
#58300=CARTESIAN_POINT ( 'NONE',  ( 24.18398860626899705, 28.73617430169804265, 5.000000000000000000 ) ) ;
#58301=VECTOR ( 'NONE', #133849, 1000.000000000000000 ) ;
#58302=CARTESIAN_POINT ( 'NONE',  ( -28.03340032343005461, 6.759292476615653023, 12.28218704918515591 ) ) ;
#58303=LINE ( 'NONE', #59014, #120261 ) ;
#58304=VERTEX_POINT ( 'NONE', #13524 ) ;
#58305=ORIENTED_EDGE ( 'NONE', *, *, #78247, .T. ) ;
#58306=AXIS2_PLACEMENT_3D ( 'NONE', #7844, #5694, #84035 ) ;
#58307=DIRECTION ( 'NONE',  ( -0.7071067811865487940, 0.7071067811865463515, 0.000000000000000000 ) ) ;
#58308=LINE ( 'NONE', #46722, #102204 ) ;
#58309=ORIENTED_EDGE ( 'NONE', *, *, #19468, .F. ) ;
#58310=ORIENTED_EDGE ( 'NONE', *, *, #99262, .F. ) ;
#58311=VERTEX_POINT ( 'NONE', #135359 ) ;
#58312=EDGE_CURVE ( 'NONE', #80179, #28705, #4038, .T. ) ;
#58313=EDGE_CURVE ( 'NONE', #122891, #76404, #136747, .T. ) ;
#58314=DIRECTION ( 'NONE',  ( 0.7071067811865487940, 0.7071067811865463515, -0.000000000000000000 ) ) ;
#58315=EDGE_LOOP ( 'NONE', ( #30835, #84652, #125698, #138659 ) ) ;
#58316=DIRECTION ( 'NONE',  ( 0.6830127018922181881, 0.6830127018922202975, -0.2588190451025214056 ) ) ;
#58317=ADVANCED_FACE ( 'NONE', ( #18516 ), #41736, .F. ) ;
#58320=LINE ( 'NONE', #122070, #21762 ) ;
#58321=ORIENTED_EDGE ( 'NONE', *, *, #109447, .T. ) ;
#58322=PLANE ( 'NONE',  #27208 ) ;
#58324=FACE_OUTER_BOUND ( 'NONE', #73251, .T. ) ;
#58325=ADVANCED_FACE ( 'NONE', ( #74383 ), #30877, .F. ) ;
#58326=CARTESIAN_POINT ( 'NONE',  ( -3.328169399223505742, 5.259292476615667233, 4.000000000000000000 ) ) ;
#58327=ORIENTED_EDGE ( 'NONE', *, *, #142251, .T. ) ;
#58328=VECTOR ( 'NONE', #43684, 1000.000000000000000 ) ;
#58329=ORIENTED_EDGE ( 'NONE', *, *, #57373, .F. ) ;
#58332=VERTEX_POINT ( 'NONE', #30129 ) ;
#58333=LINE ( 'NONE', #122085, #57420 ) ;
#58335=VECTOR ( 'NONE', #89111, 1000.000000000000000 ) ;
#58337=LINE ( 'NONE', #102520, #48704 ) ;
#58338=FACE_OUTER_BOUND ( 'NONE', #37123, .T. ) ;
#58339=EDGE_CURVE ( 'NONE', #24531, #89253, #51195, .T. ) ;
#58340=VECTOR ( 'NONE', #109625, 1000.000000000000000 ) ;
#58341=ORIENTED_EDGE ( 'NONE', *, *, #51672, .F. ) ;
#58342=DIRECTION ( 'NONE',  ( -0.7071067811865487940, 0.7071067811865463515, -0.000000000000000000 ) ) ;
#58343=DIRECTION ( 'NONE',  ( -0.000000000000000000, 0.3543493200069153248, 0.9351131265310292928 ) ) ;
#58344=CARTESIAN_POINT ( 'NONE',  ( 0.000000000000000000, 0.000000000000000000, 5.000000000000000000 ) ) ;
#58345=CARTESIAN_POINT ( 'NONE',  ( 20.35681257248249310, -20.24070752338407431, 21.22881796311217428 ) ) ;
#58346=ORIENTED_EDGE ( 'NONE', *, *, #2709, .T. ) ;
#58347=EDGE_CURVE ( 'NONE', #75683, #116329, #127301, .T. ) ;
#58348=ORIENTED_EDGE ( 'NONE', *, *, #82583, .T. ) ;
#58349=ADVANCED_FACE ( 'NONE', ( #128051 ), #40334, .T. ) ;
#58350=VECTOR ( 'NONE', #128398, 1000.000000000000000 ) ;
#58352=CARTESIAN_POINT ( 'NONE',  ( -56.99451991528749062, 28.92564299267978001, 4.000000000000000000 ) ) ;
#58353=EDGE_CURVE ( 'NONE', #25609, #49451, #73653, .T. ) ;
#58355=CARTESIAN_POINT ( 'NONE',  ( -34.49999999999976552, -2.945670655169033481, 4.994342998332163219 ) ) ;
#58356=LINE ( 'NONE', #1031, #136445 ) ;
#58357=CARTESIAN_POINT ( 'NONE',  ( 34.92499999999998295, -7.285322628117683053, -6.182564397582753557 ) ) ;
#58358=CARTESIAN_POINT ( 'NONE',  ( 39.48921356237310221, -27.52281430457082934, 5.000000000000000000 ) ) ;
#58359=ORIENTED_EDGE ( 'NONE', *, *, #14852, .T. ) ;
#58360=DIRECTION ( 'NONE',  ( 0.6830127018922180770, 0.6830127018922202975, -0.2588190451025213501 ) ) ;
#58362=VECTOR ( 'NONE', #74915, 1000.000000000000000 ) ;
#58366=DIRECTION ( 'NONE',  ( 0.7071067811865487940, 0.7071067811865463515, 0.000000000000000000 ) ) ;
#58368=AXIS2_PLACEMENT_3D ( 'NONE', #24870, #124901, #58276 ) ;
#58369=DIRECTION ( 'NONE',  ( -0.7071067811865487940, 0.7071067811865463515, -0.000000000000000000 ) ) ;
#58370=EDGE_LOOP ( 'NONE', ( #97754, #22727, #137595, #124350 ) ) ;
#58372=ORIENTED_EDGE ( 'NONE', *, *, #94851, .T. ) ;
#58373=VECTOR ( 'NONE', #61252, 1000.000000000000000 ) ;
#58374=VECTOR ( 'NONE', #130195, 1000.000000000000000 ) ;
#58377=DIRECTION ( 'NONE',  ( 1.000000000000000000, 0.000000000000000000, 0.000000000000000000 ) ) ;
#58378=DIRECTION ( 'NONE',  ( 0.3543493200069162685, -0.000000000000000000, -0.9351131265310288487 ) ) ;
#58379=LINE ( 'NONE', #92349, #64912 ) ;
#58380=CARTESIAN_POINT ( 'NONE',  ( -14.67183060077637080, 11.25929247661560595, 4.000000000000000000 ) ) ;
#58381=FACE_OUTER_BOUND ( 'NONE', #96527, .T. ) ;
#58382=ORIENTED_EDGE ( 'NONE', *, *, #46026, .T. ) ;
#58383=EDGE_LOOP ( 'NONE', ( #71470, #31278, #94081, #97365 ) ) ;
#58384=DIRECTION ( 'NONE',  ( -0.000000000000000000, 0.3543493200069153248, 0.9351131265310292928 ) ) ;
#58385=CARTESIAN_POINT ( 'NONE',  ( 28.49999999999980460, -5.568876922607759461, 4.000000000000000000 ) ) ;
#58386=DIRECTION ( 'NONE',  ( -0.000000000000000000, -0.3543493200069152693, 0.9351131265310292928 ) ) ;
#58387=DIRECTION ( 'NONE',  ( -0.7071067811865486830, -0.7071067811865464625, 0.000000000000000000 ) ) ;
#58389=CARTESIAN_POINT ( 'NONE',  ( -19.82816939922339472, -8.240707523384191546, 4.000000000000000000 ) ) ;
#58390=DIRECTION ( 'NONE',  ( -0.7071067811865486830, -0.7071067811865464625, 0.000000000000000000 ) ) ;
#58391=ORIENTED_EDGE ( 'NONE', *, *, #47607, .T. ) ;
#58393=CARTESIAN_POINT ( 'NONE',  ( -27.48921356237309155, -27.52281430457074762, 5.000000000000000000 ) ) ;
#58394=CARTESIAN_POINT ( 'NONE',  ( -25.49999999999981526, -7.533600742197664069, 5.000000000000000000 ) ) ;
#58396=VERTEX_POINT ( 'NONE', #8348 ) ;
#58398=CARTESIAN_POINT ( 'NONE',  ( -16.82816939922340893, 21.75929247661550647, 4.000000000000000000 ) ) ;
#58400=DIRECTION ( 'NONE',  ( -0.6830127018922181881, 0.6830127018922202975, -0.2588190451025214056 ) ) ;
#58402=VECTOR ( 'NONE', #55788, 999.9999999999998863 ) ;
#58403=LINE ( 'NONE', #111984, #117699 ) ;
#58405=ORIENTED_EDGE ( 'NONE', *, *, #28442, .T. ) ;
#58406=VECTOR ( 'NONE', #36416, 1000.000000000000227 ) ;
#58407=LINE ( 'NONE', #62646, #12900 ) ;
#58409=EDGE_CURVE ( 'NONE', #87440, #56693, #128736, .T. ) ;
#58410=DIRECTION ( 'NONE',  ( 0.7071067811865487940, 0.7071067811865463515, 0.000000000000000000 ) ) ;
#58413=EDGE_CURVE ( 'NONE', #108755, #15722, #139655, .T. ) ;
#58414=DIRECTION ( 'NONE',  ( 0.7071067811865487940, 0.7071067811865463515, 0.000000000000000000 ) ) ;
#58416=DIRECTION ( 'NONE',  ( 0.7071067811865486830, -0.7071067811865464625, -0.000000000000000000 ) ) ;
#58417=VECTOR ( 'NONE', #129912, 1000.000000000000000 ) ;
#58419=ORIENTED_EDGE ( 'NONE', *, *, #3710, .T. ) ;
#58420=ORIENTED_EDGE ( 'NONE', *, *, #113496, .T. ) ;
#58422=ORIENTED_EDGE ( 'NONE', *, *, #116656, .F. ) ;
#58423=ADVANCED_FACE ( 'NONE', ( #72272 ), #52599, .F. ) ;
#58424=PLANE ( 'NONE',  #96167 ) ;
#58425=LINE ( 'NONE', #101149, #78811 ) ;
#58426=CARTESIAN_POINT ( 'NONE',  ( 17.20710678118642889, -11.24070752338416668, 5.000000000000000000 ) ) ;
#58430=EDGE_LOOP ( 'NONE', ( #47775, #20356, #90, #66760, #3793, #125945 ) ) ;
#58432=AXIS2_PLACEMENT_3D ( 'NONE', #76890, #66701, #44995 ) ;
#58433=FACE_OUTER_BOUND ( 'NONE', #18295, .T. ) ;
#58435=EDGE_CURVE ( 'NONE', #95865, #105802, #38878, .T. ) ;
#58436=ORIENTED_EDGE ( 'NONE', *, *, #42419, .T. ) ;
#58437=CARTESIAN_POINT ( 'NONE',  ( -19.17183060077633172, 9.759292476615618384, 4.000000000000000000 ) ) ;
#58438=EDGE_LOOP ( 'NONE', ( #7474, #89482, #113677, #102523 ) ) ;
#58439=FACE_OUTER_BOUND ( 'NONE', #38031, .T. ) ;
#58440=DIRECTION ( 'NONE',  ( 0.6830127018922180770, -0.6830127018922204085, -0.2588190451025213501 ) ) ;
#58441=AXIS2_PLACEMENT_3D ( 'NONE', #127467, #37629, #82546 ) ;
#58444=ORIENTED_EDGE ( 'NONE', *, *, #128641, .T. ) ;
#58445=FACE_BOUND ( 'NONE', #35712, .T. ) ;
#58446=LINE ( 'NONE', #11275, #15427 ) ;
#58447=PLANE ( 'NONE',  #74470 ) ;
#58449=VECTOR ( 'NONE', #79604, 1000.000000000000000 ) ;
#58450=CARTESIAN_POINT ( 'NONE',  ( -5.999999999999956479, 12.25461709320620507, -10.07315571508698682 ) ) ;
#58451=CARTESIAN_POINT ( 'NONE',  ( 34.92499999999998295, 22.22500000000000142, 4.000000000000000000 ) ) ;
#58453=VERTEX_POINT ( 'NONE', #106977 ) ;
#58454=ORIENTED_EDGE ( 'NONE', *, *, #114859, .T. ) ;
#58456=ORIENTED_EDGE ( 'NONE', *, *, #125138, .T. ) ;
#58458=ORIENTED_EDGE ( 'NONE', *, *, #37309, .T. ) ;
#58459=EDGE_CURVE ( 'NONE', #98731, #81677, #64208, .T. ) ;
#58460=CARTESIAN_POINT ( 'NONE',  ( 0.000000000000000000, 0.000000000000000000, 5.000000000000000000 ) ) ;
#58465=EDGE_CURVE ( 'NONE', #141981, #8088, #7656, .T. ) ;
#58467=EDGE_CURVE ( 'NONE', #129514, #91137, #6198, .T. ) ;
#58469=CARTESIAN_POINT ( 'NONE',  ( 25.93003974513575827, -0.7407075233842770334, 13.87443053587604780 ) ) ;
#58471=DIRECTION ( 'NONE',  ( -0.7071067811865486830, -0.7071067811865464625, -0.000000000000000000 ) ) ;
#58475=CARTESIAN_POINT ( 'NONE',  ( 12.48921356237309155, -27.52281430457064104, 5.000000000000000000 ) ) ;
#58477=AXIS2_PLACEMENT_3D ( 'NONE', #135207, #38021, #71355 ) ;
#58478=FACE_OUTER_BOUND ( 'NONE', #118574, .T. ) ;
#58479=ORIENTED_EDGE ( 'NONE', *, *, #117888, .F. ) ;
#58480=EDGE_CURVE ( 'NONE', #67347, #87818, #116440, .T. ) ;
#58481=LINE ( 'NONE', #2583, #139889 ) ;
#58482=CARTESIAN_POINT ( 'NONE',  ( -17.51078643762690845, -27.52281430457043143, 5.000000000000000000 ) ) ;
#58483=EDGE_LOOP ( 'NONE', ( #78947, #53615, #70083 ) ) ;
#58484=EDGE_LOOP ( 'NONE', ( #138496, #126193, #76192, #46017 ) ) ;
#58485=EDGE_CURVE ( 'NONE', #25524, #30424, #50475, .T. ) ;
#58486=EDGE_CURVE ( 'NONE', #17176, #115135, #17810, .T. ) ;
#58487=VERTEX_POINT ( 'NONE', #32296 ) ;
#58491=LINE ( 'NONE', #1852, #137461 ) ;
#58492=EDGE_CURVE ( 'NONE', #13019, #141546, #100407, .T. ) ;
#58493=ORIENTED_EDGE ( 'NONE', *, *, #103164, .T. ) ;
#58494=DIRECTION ( 'NONE',  ( -0.000000000000000000, 0.3543493200069153248, 0.9351131265310292928 ) ) ;
#58495=ORIENTED_EDGE ( 'NONE', *, *, #91118, .T. ) ;
#58497=EDGE_CURVE ( 'NONE', #102967, #90134, #132349, .T. ) ;
#58498=CARTESIAN_POINT ( 'NONE',  ( 63.48921356237309510, -27.52281430457099631, 5.000000000000000000 ) ) ;
#58499=ORIENTED_EDGE ( 'NONE', *, *, #37100, .F. ) ;
#58500=VECTOR ( 'NONE', #105131, 1000.000000000000227 ) ;
#58501=LINE ( 'NONE', #70773, #138693 ) ;
#58502=CARTESIAN_POINT ( 'NONE',  ( -48.18398860626899705, 28.73617430169820608, 5.000000000000000000 ) ) ;
#58503=ORIENTED_EDGE ( 'NONE', *, *, #16856, .T. ) ;
#58504=CARTESIAN_POINT ( 'NONE',  ( 13.49999999999990763, -16.53360074219757081, 5.000000000000000000 ) ) ;
#58506=VECTOR ( 'NONE', #134609, 1000.000000000000000 ) ;
#58507=ORIENTED_EDGE ( 'NONE', *, *, #18787, .F. ) ;
#58508=ORIENTED_EDGE ( 'NONE', *, *, #114779, .T. ) ;
#58509=CARTESIAN_POINT ( 'NONE',  ( -54.29974487139159578, -27.71228299555243879, 4.000000000000000000 ) ) ;
#58510=VECTOR ( 'NONE', #63721, 1000.000000000000227 ) ;
#58511=PLANE ( 'NONE',  #19118 ) ;
#58512=CARTESIAN_POINT ( 'NONE',  ( 53.99451991528749062, 28.92564299267975869, 4.000000000000000000 ) ) ;
#58513=FACE_OUTER_BOUND ( 'NONE', #62842, .T. ) ;
#58514=CARTESIAN_POINT ( 'NONE',  ( 14.81601139373099585, 28.73617430169776910, 5.000000000000000000 ) ) ;
#58515=ORIENTED_EDGE ( 'NONE', *, *, #97353, .F. ) ;
#58516=EDGE_CURVE ( 'NONE', #18784, #11268, #88098, .T. ) ;
#58518=EDGE_CURVE ( 'NONE', #17485, #130029, #45339, .T. ) ;
#58519=EDGE_CURVE ( 'NONE', #78029, #5674, #99664, .T. ) ;
#58521=DIRECTION ( 'NONE',  ( 1.000000000000000000, 0.000000000000000000, 0.000000000000000000 ) ) ;
#58524=ORIENTED_EDGE ( 'NONE', *, *, #112617, .T. ) ;
#58525=ORIENTED_EDGE ( 'NONE', *, *, #63146, .F. ) ;
#58527=EDGE_LOOP ( 'NONE', ( #60234, #64620, #32326, #136508 ) ) ;
#58528=CARTESIAN_POINT ( 'NONE',  ( 14.29298673570684919, -21.74070752338406365, 4.999753212805221558 ) ) ;
#58529=LINE ( 'NONE', #113543, #99701 ) ;
#58530=VECTOR ( 'NONE', #47672, 1000.000000000000114 ) ;
#58535=FACE_OUTER_BOUND ( 'NONE', #28145, .T. ) ;
#58537=CARTESIAN_POINT ( 'NONE',  ( -10.82816939922344979, -8.240707523384198652, 4.000000000000000000 ) ) ;
#58538=LINE ( 'NONE', #93955, #20037 ) ;
#58539=CARTESIAN_POINT ( 'NONE',  ( 0.000000000000000000, 0.000000000000000000, 5.000000000000000000 ) ) ;
#58540=LINE ( 'NONE', #116957, #81388 ) ;
#58542=ORIENTED_EDGE ( 'NONE', *, *, #30221, .T. ) ;
#58543=VECTOR ( 'NONE', #91041, 1000.000000000000000 ) ;
#58544=LINE ( 'NONE', #102712, #61502 ) ;
#58545=ORIENTED_EDGE ( 'NONE', *, *, #17898, .F. ) ;
#58547=DIRECTION ( 'NONE',  ( 1.000000000000000000, 0.000000000000000000, 0.000000000000000000 ) ) ;
#58548=CARTESIAN_POINT ( 'NONE',  ( 18.72281430457046270, -21.72500000000000142, 5.000000000000000000 ) ) ;
#58549=ORIENTED_EDGE ( 'NONE', *, *, #37249, .T. ) ;
#58551=FACE_OUTER_BOUND ( 'NONE', #12355, .T. ) ;
#58552=ORIENTED_EDGE ( 'NONE', *, *, #120443, .F. ) ;
#58553=LINE ( 'NONE', #91147, #41569 ) ;
#58555=ORIENTED_EDGE ( 'NONE', *, *, #28457, .T. ) ;
#58556=LINE ( 'NONE', #6207, #442 ) ;
#58557=ORIENTED_EDGE ( 'NONE', *, *, #54175, .F. ) ;
#58558=CARTESIAN_POINT ( 'NONE',  ( -24.48921356237309510, -27.52281430457072631, 5.000000000000000000 ) ) ;
#58560=CARTESIAN_POINT ( 'NONE',  ( 8.816011393731004731, 28.73617430169781173, 5.000000000000000000 ) ) ;
#58561=LINE ( 'NONE', #44823, #126946 ) ;
#58562=EDGE_LOOP ( 'NONE', ( #133826, #131705, #35025, #133061 ) ) ;
#58563=CARTESIAN_POINT ( 'NONE',  ( 22.49999999999984368, -10.04351517176476172, -1.623559851933770171 ) ) ;
#58564=PLANE ( 'NONE',  #119052 ) ;
#58565=ADVANCED_FACE ( 'NONE', ( #340 ), #78649, .T. ) ;
#58568=CARTESIAN_POINT ( 'NONE',  ( -8.999999999999934275, -9.033600742197648970, 5.000000000000000000 ) ) ;
#58569=AXIS2_PLACEMENT_3D ( 'NONE', #118355, #73456, #127845 ) ;
#58571=DIRECTION ( 'NONE',  ( 0.7071067811865487940, 0.7071067811865463515, 0.000000000000000000 ) ) ;
#58573=AXIS2_PLACEMENT_3D ( 'NONE', #138523, #119586, #18862 ) ;
#58574=VECTOR ( 'NONE', #16300, 1000.000000000000000 ) ;
#58575=FACE_OUTER_BOUND ( 'NONE', #43717, .T. ) ;
#58576=VERTEX_POINT ( 'NONE', #21415 ) ;
#58578=PLANE ( 'NONE',  #50124 ) ;
#58580=CARTESIAN_POINT ( 'NONE',  ( 28.49999999999980105, -12.66682484999663671, -0.6294897503863281507 ) ) ;
#58581=AXIS2_PLACEMENT_3D ( 'NONE', #79616, #33243, #91176 ) ;
#58582=FACE_OUTER_BOUND ( 'NONE', #83971, .T. ) ;
#58584=EDGE_CURVE ( 'NONE', #36068, #110646, #44637, .T. ) ;
#58585=DIRECTION ( 'NONE',  ( -0.000000000000000000, -0.3543493200069152693, 0.9351131265310292928 ) ) ;
#58586=VERTEX_POINT ( 'NONE', #10508 ) ;
#58588=ADVANCED_FACE ( 'NONE', ( #34425 ), #43887, .F. ) ;
#58589=LINE ( 'NONE', #91188, #126201 ) ;
#58590=ORIENTED_EDGE ( 'NONE', *, *, #118641, .T. ) ;
#58591=FACE_OUTER_BOUND ( 'NONE', #45548, .T. ) ;
#58592=CARTESIAN_POINT ( 'NONE',  ( 4.499999999999968914, -12.66682484999666158, -0.6294897503863827737 ) ) ;
#58593=LINE ( 'NONE', #125220, #16895 ) ;
#58594=EDGE_CURVE ( 'NONE', #52857, #60630, #64926, .T. ) ;
#58596=EDGE_CURVE ( 'NONE', #62444, #10426, #75803, .T. ) ;
#58597=ORIENTED_EDGE ( 'NONE', *, *, #9473, .F. ) ;
#58600=AXIS2_PLACEMENT_3D ( 'NONE', #139640, #30863, #141011 ) ;
#58601=ORIENTED_EDGE ( 'NONE', *, *, #54833, .T. ) ;
#58602=ADVANCED_FACE ( 'NONE', ( #9808 ), #98264, .T. ) ;
#58604=CARTESIAN_POINT ( 'NONE',  ( -66.29974487139159578, -27.71228299555252406, 4.000000000000000000 ) ) ;
#58605=DIRECTION ( 'NONE',  ( -0.7071067811865486830, 0.7071067811865464625, 0.000000000000000000 ) ) ;
#58606=CARTESIAN_POINT ( 'NONE',  ( 29.99451991528749417, 28.92564299267958816, 4.000000000000000000 ) ) ;
#58607=VERTEX_POINT ( 'NONE', #88827 ) ;
#58608=DIRECTION ( 'NONE',  ( -0.6830127018922181881, 0.6830127018922202975, -0.2588190451025214056 ) ) ;
#58609=CARTESIAN_POINT ( 'NONE',  ( 39.85005128541000374, -8.240707523384182664, 17.25253755692248347 ) ) ;
#58610=AXIS2_PLACEMENT_3D ( 'NONE', #4887, #35467, #15758 ) ;
#58612=CARTESIAN_POINT ( 'NONE',  ( 28.11017322888191217, -22.22500000000000142, 4.785647885939353863 ) ) ;
#58614=VERTEX_POINT ( 'NONE', #121422 ) ;
#58616=DIRECTION ( 'NONE',  ( 0.7071067811865487940, -0.7071067811865463515, 0.000000000000000000 ) ) ;
#58618=DIRECTION ( 'NONE',  ( 0.6830127018922181881, 0.6830127018922202975, -0.2588190451025214056 ) ) ;
#58619=CARTESIAN_POINT ( 'NONE',  ( 60.48921356237309510, -27.52281430457097500, 5.000000000000000000 ) ) ;
#58620=AXIS2_PLACEMENT_3D ( 'NONE', #45554, #112216, #78160 ) ;
#58621=EDGE_CURVE ( 'NONE', #116708, #7217, #110528, .T. ) ;
#58622=ORIENTED_EDGE ( 'NONE', *, *, #126643, .F. ) ;
#58623=ORIENTED_EDGE ( 'NONE', *, *, #15017, .F. ) ;
#58625=DIRECTION ( 'NONE',  ( -0.3543493200069162685, -0.000000000000000000, -0.9351131265310288487 ) ) ;
#58627=CARTESIAN_POINT ( 'NONE',  ( -7.171830600776425868, -20.24070752338407786, 4.000000000000000000 ) ) ;
#58628=EDGE_CURVE ( 'NONE', #69257, #130179, #55480, .T. ) ;
#58630=CARTESIAN_POINT ( 'NONE',  ( -21.29974487139158512, -27.71228299555221142, 4.000000000000000000 ) ) ;
#58631=VECTOR ( 'NONE', #73293, 999.9999999999998863 ) ;
#58632=DIRECTION ( 'NONE',  ( -0.7071067811865486830, 0.7071067811865464625, 0.000000000000000000 ) ) ;
#58634=EDGE_LOOP ( 'NONE', ( #103445, #132115, #91752, #142446 ) ) ;
#58635=ORIENTED_EDGE ( 'NONE', *, *, #13230, .F. ) ;
#58636=DIRECTION ( 'NONE',  ( -0.7071067811865486830, -0.7071067811865464625, -0.000000000000000000 ) ) ;
#58637=ORIENTED_EDGE ( 'NONE', *, *, #46870, .F. ) ;
#58638=VECTOR ( 'NONE', #23626, 1000.000000000000000 ) ;
#58639=ADVANCED_FACE ( 'NONE', ( #122129 ), #56226, .T. ) ;
#58641=EDGE_CURVE ( 'NONE', #80628, #13922, #59077, .T. ) ;
#58642=FACE_OUTER_BOUND ( 'NONE', #64561, .T. ) ;
#58643=ORIENTED_EDGE ( 'NONE', *, *, #23556, .T. ) ;
#58645=CARTESIAN_POINT ( 'NONE',  ( -34.49999999999975842, -11.56887692260769640, 4.000000000000000000 ) ) ;
#58646=EDGE_CURVE ( 'NONE', #83534, #23652, #126412, .T. ) ;
#58649=DIRECTION ( 'NONE',  ( -0.7071067811865486830, -0.7071067811865464625, 0.000000000000000000 ) ) ;
#58651=ADVANCED_FACE ( 'NONE', ( #91656 ), #46787, .F. ) ;
#58655=DIRECTION ( 'NONE',  ( -0.7071067811865486830, 0.7071067811865464625, 0.000000000000000000 ) ) ;
#58656=ORIENTED_EDGE ( 'NONE', *, *, #26350, .F. ) ;
#58657=ORIENTED_EDGE ( 'NONE', *, *, #56967, .T. ) ;
#58658=CARTESIAN_POINT ( 'NONE',  ( 17.29289321881334018, 17.25929247661554911, 5.000000000000000000 ) ) ;
#58659=ORIENTED_EDGE ( 'NONE', *, *, #138161, .T. ) ;
#58660=ORIENTED_EDGE ( 'NONE', *, *, #43030, .T. ) ;
#58661=DIRECTION ( 'NONE',  ( -0.7071067811865486830, -0.7071067811865464625, 0.000000000000000000 ) ) ;
#58663=LINE ( 'NONE', #14380, #120614 ) ;
#58664=LINE ( 'NONE', #57208, #125943 ) ;
#58666=DIRECTION ( 'NONE',  ( -0.7071067811865486830, -0.7071067811865464625, 0.000000000000000000 ) ) ;
#58668=DIRECTION ( 'NONE',  ( -0.000000000000000000, 0.3543493200069153248, 0.9351131265310292928 ) ) ;
#58669=CARTESIAN_POINT ( 'NONE',  ( -22.49999999999984368, -2.947814304570797184, 5.000000000000000000 ) ) ;
#58670=VECTOR ( 'NONE', #21013, 1000.000000000000227 ) ;
#58671=EDGE_CURVE ( 'NONE', #27773, #51825, #125734, .T. ) ;
#58672=DIRECTION ( 'NONE',  ( 1.000000000000000000, 0.000000000000000000, 0.000000000000000000 ) ) ;
#58675=LINE ( 'NONE', #123893, #13286 ) ;
#58676=PLANE ( 'NONE',  #26793 ) ;
#58678=ORIENTED_EDGE ( 'NONE', *, *, #90641, .T. ) ;
#58679=VECTOR ( 'NONE', #13229, 1000.000000000000000 ) ;
#58681=CARTESIAN_POINT ( 'NONE',  ( -14.99999999999989342, -13.97847968911261596, -0.1324546996127147214 ) ) ;
#58683=VECTOR ( 'NONE', #22721, 1000.000000000000000 ) ;
#58684=CARTESIAN_POINT ( 'NONE',  ( -3.299744871391591339, -27.71228299555208352, 4.000000000000000000 ) ) ;
#58685=CARTESIAN_POINT ( 'NONE',  ( 9.831811731255163167, 22.22500000000000142, 21.96002906245333008 ) ) ;
#58686=PLANE ( 'NONE',  #9202 ) ;
#58687=CARTESIAN_POINT ( 'NONE',  ( 3.707106781186521705, -6.740707523384207533, 5.000000000000000000 ) ) ;
#58689=ORIENTED_EDGE ( 'NONE', *, *, #4006, .F. ) ;
#58690=LINE ( 'NONE', #123906, #13966 ) ;
#58691=EDGE_LOOP ( 'NONE', ( #125326, #41688, #112226, #118090 ) ) ;
#58693=EDGE_CURVE ( 'NONE', #87786, #108114, #4576, .T. ) ;
#58696=VERTEX_POINT ( 'NONE', #103234 ) ;
#58698=FACE_OUTER_BOUND ( 'NONE', #66158, .T. ) ;
#58699=VERTEX_POINT ( 'NONE', #137318 ) ;
#58700=ORIENTED_EDGE ( 'NONE', *, *, #133673, .T. ) ;
#58701=EDGE_LOOP ( 'NONE', ( #122353, #111790, #117083, #31124 ) ) ;
#58704=LINE ( 'NONE', #125332, #102964 ) ;
#58705=CARTESIAN_POINT ( 'NONE',  ( -27.48921356237309155, -27.52281430457074762, 5.000000000000000000 ) ) ;
#58708=DIRECTION ( 'NONE',  ( -0.6830127018922180770, -0.6830127018922204085, -0.2588190451025213501 ) ) ;
#58710=EDGE_CURVE ( 'NONE', #4252, #108455, #70658, .T. ) ;
#58711=VECTOR ( 'NONE', #93761, 1000.000000000000227 ) ;
#58712=LINE ( 'NONE', #26728, #7151 ) ;
#58713=DIRECTION ( 'NONE',  ( 0.7071067811865487940, 0.7071067811865463515, 0.000000000000000000 ) ) ;
#58714=ORIENTED_EDGE ( 'NONE', *, *, #126843, .T. ) ;
#58716=VERTEX_POINT ( 'NONE', #37284 ) ;
#58717=VECTOR ( 'NONE', #140297, 1000.000000000000000 ) ;
#58718=DIRECTION ( 'NONE',  ( -0.6830127018922180770, -0.6830127018922204085, -0.2588190451025213501 ) ) ;
#58719=VERTEX_POINT ( 'NONE', #114803 ) ;
#58720=EDGE_LOOP ( 'NONE', ( #140974, #13582, #37891, #106139 ) ) ;
#58721=EDGE_CURVE ( 'NONE', #40729, #128263, #80799, .T. ) ;
#58722=FACE_OUTER_BOUND ( 'NONE', #127592, .T. ) ;
#58723=FACE_OUTER_BOUND ( 'NONE', #78685, .T. ) ;
#58724=ORIENTED_EDGE ( 'NONE', *, *, #112424, .T. ) ;
#58726=ORIENTED_EDGE ( 'NONE', *, *, #90691, .T. ) ;
#58727=( BOUNDED_CURVE ( )  B_SPLINE_CURVE ( 3, ( #8343, #98259, #7649, #19261 ),
 .UNSPECIFIED., .F., .T. ) 
 B_SPLINE_CURVE_WITH_KNOTS ( ( 4, 4 ),
 ( 5.255487504216517003, 5.308805501018120765 ),
 .UNSPECIFIED. ) 
 CURVE ( )  GEOMETRIC_REPRESENTATION_ITEM ( )  RATIONAL_B_SPLINE_CURVE ( ( 1.000000000000000000, 0.9997631132982454094, 0.9997631132982454094, 1.000000000000000000 ) ) 
 REPRESENTATION_ITEM ( '' )  );
#58728=VECTOR ( 'NONE', #117053, 1000.000000000000000 ) ;
#58729=LINE ( 'NONE', #84023, #54521 ) ;
#58730=LINE ( 'NONE', #111626, #48555 ) ;
#58731=PLANE ( 'NONE',  #36899 ) ;
#58732=LINE ( 'NONE', #23153, #127165 ) ;
#58734=DIRECTION ( 'NONE',  ( 0.7071067811865486830, -0.7071067811865464625, -0.000000000000000000 ) ) ;
#58735=CARTESIAN_POINT ( 'NONE',  ( -56.99451991528749062, 28.92564299267978001, 4.000000000000000000 ) ) ;
#58737=CARTESIAN_POINT ( 'NONE',  ( 0.7071067811865406894, 14.25929247661556865, 5.000000000000000000 ) ) ;
#58739=CARTESIAN_POINT ( 'NONE',  ( -51.48921356237309510, -27.52281430457091460, 5.000000000000000000 ) ) ;
#58740=CARTESIAN_POINT ( 'NONE',  ( -42.48921356237308800, -27.52281430457085065, 5.000000000000000000 ) ) ;
#58741=DIRECTION ( 'NONE',  ( 0.7071067811865487940, -0.7071067811865463515, 0.000000000000000000 ) ) ;
#58742=ORIENTED_EDGE ( 'NONE', *, *, #15182, .F. ) ;
#58743=ORIENTED_EDGE ( 'NONE', *, *, #73760, .T. ) ;
#58745=VERTEX_POINT ( 'NONE', #15483 ) ;
#58748=EDGE_CURVE ( 'NONE', #97422, #139654, #26412, .T. ) ;
#58749=DIRECTION ( 'NONE',  ( 0.000000000000000000, 0.3543493200069153248, 0.9351131265310291818 ) ) ;
#58750=VECTOR ( 'NONE', #79479, 1000.000000000000000 ) ;
#58752=ORIENTED_EDGE ( 'NONE', *, *, #85443, .F. ) ;
#58753=CARTESIAN_POINT ( 'NONE',  ( -25.49999999999981881, 16.08746187583908238, 4.000000000000000000 ) ) ;
#58754=LINE ( 'NONE', #79062, #11663 ) ;
#58755=DIRECTION ( 'NONE',  ( 0.6830127018922181881, 0.6830127018922202975, -0.2588190451025214056 ) ) ;
#58757=EDGE_CURVE ( 'NONE', #95983, #16, #79411, .T. ) ;
#58758=EDGE_CURVE ( 'NONE', #38910, #142123, #124998, .T. ) ;
#58759=DIRECTION ( 'NONE',  ( -0.000000000000000000, 0.000000000000000000, 1.000000000000000000 ) ) ;
#58760=DIRECTION ( 'NONE',  ( -0.3543493200069163795, -9.265275131829747941E-33, -0.9351131265310288487 ) ) ;
#58762=CARTESIAN_POINT ( 'NONE',  ( -0.2997448713915885632, -27.71228299555206220, 4.000000000000000000 ) ) ;
#58765=PLANE ( 'NONE',  #103153 ) ;
#58767=EDGE_CURVE ( 'NONE', #132252, #85524, #25677, .T. ) ;
#58769=ORIENTED_EDGE ( 'NONE', *, *, #22321, .F. ) ;
#58770=ORIENTED_EDGE ( 'NONE', *, *, #131545, .F. ) ;
#58773=EDGE_CURVE ( 'NONE', #5681, #94085, #40847, .T. ) ;
#58774=ORIENTED_EDGE ( 'NONE', *, *, #93606, .T. ) ;
#58775=ADVANCED_FACE ( 'NONE', ( #95932 ), #85057, .F. ) ;
#58777=ADVANCED_FACE ( 'NONE', ( #49620 ), #28557, .F. ) ;
#58779=VERTEX_POINT ( 'NONE', #29244 ) ;
#58781=CARTESIAN_POINT ( 'NONE',  ( -31.49999999999977973, -8.568876922607721269, 4.000000000000000000 ) ) ;
#58782=AXIS2_PLACEMENT_3D ( 'NONE', #123145, #67333, #89766 ) ;
#58783=ADVANCED_FACE ( 'NONE', ( #61230 ), #95214, .T. ) ;
#58785=ORIENTED_EDGE ( 'NONE', *, *, #133178, .F. ) ;
#58786=EDGE_LOOP ( 'NONE', ( #56482, #40758, #140997, #137888 ) ) ;
#58787=CARTESIAN_POINT ( 'NONE',  ( 23.20710678118638270, -5.240707523384235955, 5.000000000000000000 ) ) ;
#58788=DIRECTION ( 'NONE',  ( 0.7071067811865487940, 0.7071067811865463515, 0.000000000000000000 ) ) ;
#58790=EDGE_CURVE ( 'NONE', #33966, #87892, #61909, .T. ) ;
#58792=ORIENTED_EDGE ( 'NONE', *, *, #143166, .F. ) ;
#58793=ORIENTED_EDGE ( 'NONE', *, *, #88181, .T. ) ;
#58794=DIRECTION ( 'NONE',  ( -1.000000000000000000, 0.000000000000000000, -0.000000000000000000 ) ) ;
#58797=EDGE_CURVE ( 'NONE', #11322, #132762, #6030, .T. ) ;
#58798=VECTOR ( 'NONE', #76718, 1000.000000000000000 ) ;
#58799=DIRECTION ( 'NONE',  ( -1.000000000000000000, 0.000000000000000000, 0.000000000000000000 ) ) ;
#58800=EDGE_LOOP ( 'NONE', ( #118493, #18831, #27401, #18518 ) ) ;
#58801=EDGE_LOOP ( 'NONE', ( #143549, #127194, #102267, #68386 ) ) ;
#58803=EDGE_LOOP ( 'NONE', ( #73315, #94126, #61483, #6327 ) ) ;
#58804=ORIENTED_EDGE ( 'NONE', *, *, #84800, .T. ) ;
#58805=AXIS2_PLACEMENT_3D ( 'NONE', #39386, #106742, #95882 ) ;
#58806=FACE_OUTER_BOUND ( 'NONE', #70636, .T. ) ;
#58807=EDGE_CURVE ( 'NONE', #22013, #38542, #116969, .T. ) ;
#58808=PLANE ( 'NONE',  #123984 ) ;
#58809=LINE ( 'NONE', #126836, #95160 ) ;
#58810=VERTEX_POINT ( 'NONE', #6734 ) ;
#58811=VECTOR ( 'NONE', #87875, 1000.000000000000000 ) ;
#58812=DIRECTION ( 'NONE',  ( 1.000000000000000000, 0.000000000000000000, 0.000000000000000000 ) ) ;
#58814=EDGE_CURVE ( 'NONE', #38978, #94114, #38708, .T. ) ;
#58815=ADVANCED_FACE ( 'NONE', ( #129998 ), #30707, .F. ) ;
#58817=FACE_BOUND ( 'NONE', #22034, .T. ) ;
#58818=ORIENTED_EDGE ( 'NONE', *, *, #44082, .F. ) ;
#58819=DIRECTION ( 'NONE',  ( 0.7071067811865487940, 0.7071067811865463515, -0.000000000000000000 ) ) ;
#58820=LINE ( 'NONE', #114553, #127123 ) ;
#58821=DIRECTION ( 'NONE',  ( -0.7071067811865486830, -0.7071067811865464625, 0.000000000000000000 ) ) ;
#58822=VERTEX_POINT ( 'NONE', #116265 ) ;
#58823=CARTESIAN_POINT ( 'NONE',  ( -34.42500000000001137, -16.45860074219782021, 5.000000000000000000 ) ) ;
#58825=ORIENTED_EDGE ( 'NONE', *, *, #37225, .T. ) ;
#58826=VECTOR ( 'NONE', #113552, 1000.000000000000000 ) ;
#58827=VERTEX_POINT ( 'NONE', #94493 ) ;
#58828=VECTOR ( 'NONE', #77854, 1000.000000000000000 ) ;
#58830=AXIS2_PLACEMENT_3D ( 'NONE', #13821, #16705, #58850 ) ;
#58831=VERTEX_POINT ( 'NONE', #117651 ) ;
#58832=CARTESIAN_POINT ( 'NONE',  ( -66.48921356237309510, -27.52281430457101763, 5.000000000000000000 ) ) ;
#58834=LINE ( 'NONE', #26152, #84304 ) ;
#58836=EDGE_LOOP ( 'NONE', ( #112237, #142416, #84007, #81960 ) ) ;
#58840=DIRECTION ( 'NONE',  ( -0.000000000000000000, -0.3543493200069152693, 0.9351131265310292928 ) ) ;
#58841=LINE ( 'NONE', #137785, #111109 ) ;
#58842=CARTESIAN_POINT ( 'NONE',  ( 6.299744871391586898, -27.71228299555210484, 4.000000000000000000 ) ) ;
#58843=EDGE_CURVE ( 'NONE', #114851, #16457, #18336, .T. ) ;
#58844=DIRECTION ( 'NONE',  ( -0.000000000000000000, 0.3543493200069152138, -0.9351131265310292928 ) ) ;
#58845=EDGE_LOOP ( 'NONE', ( #106424, #49351, #69064, #128782 ) ) ;
#58846=EDGE_LOOP ( 'NONE', ( #91644, #33827, #138320, #3522 ) ) ;
#58847=VECTOR ( 'NONE', #74338, 999.9999999999998863 ) ;
#58848=ORIENTED_EDGE ( 'NONE', *, *, #46982, .F. ) ;
#58849=ORIENTED_EDGE ( 'NONE', *, *, #1606, .F. ) ;
#58850=DIRECTION ( 'NONE',  ( -0.7071067811865486830, -0.7071067811865464625, 0.000000000000000000 ) ) ;
#58853=CARTESIAN_POINT ( 'NONE',  ( 34.92499999999998295, 22.22500000000000142, 4.500000000000000888 ) ) ;
#58855=CARTESIAN_POINT ( 'NONE',  ( 36.48921356237310221, -27.52281430457080802, 5.000000000000000000 ) ) ;
#58856=VERTEX_POINT ( 'NONE', #32851 ) ;
#58858=ORIENTED_EDGE ( 'NONE', *, *, #55094, .F. ) ;
#58859=LINE ( 'NONE', #13834, #88437 ) ;
#58860=EDGE_CURVE ( 'NONE', #56792, #20176, #879, .T. ) ;
#58861=LINE ( 'NONE', #71126, #126044 ) ;
#58862=VECTOR ( 'NONE', #35108, 1000.000000000000114 ) ;
#58864=ORIENTED_EDGE ( 'NONE', *, *, #97745, .F. ) ;
#58866=DIRECTION ( 'NONE',  ( 1.000000000000000000, 0.000000000000000000, 0.000000000000000000 ) ) ;
#58868=CARTESIAN_POINT ( 'NONE',  ( -2.671830600776444964, -18.74070752338408852, 4.000000000000000000 ) ) ;
#58870=ORIENTED_EDGE ( 'NONE', *, *, #55806, .T. ) ;
#58871=ORIENTED_EDGE ( 'NONE', *, *, #70379, .T. ) ;
#58872=ORIENTED_EDGE ( 'NONE', *, *, #77054, .T. ) ;
#58873=CARTESIAN_POINT ( 'NONE',  ( 0.000000000000000000, 0.000000000000000000, 5.000000000000000000 ) ) ;
#58874=LINE ( 'NONE', #47971, #41845 ) ;
#58875=FACE_OUTER_BOUND ( 'NONE', #114373, .T. ) ;
#58881=ADVANCED_FACE ( 'NONE', ( #132884 ), #32111, .F. ) ;
#58882=CARTESIAN_POINT ( 'NONE',  ( -2.700255128608413990, -27.71228299555204089, 4.000000000000000000 ) ) ;
#58883=EDGE_CURVE ( 'NONE', #31464, #19753, #131433, .T. ) ;
#58885=DIRECTION ( 'NONE',  ( -0.7071067811865486830, 0.7071067811865464625, 0.000000000000000000 ) ) ;
#58886=ORIENTED_EDGE ( 'NONE', *, *, #115866, .F. ) ;
#58887=DIRECTION ( 'NONE',  ( 0.6830127018922181881, 0.6830127018922202975, -0.2588190451025214056 ) ) ;
#58889=ORIENTED_EDGE ( 'NONE', *, *, #11458, .T. ) ;
#58890=CARTESIAN_POINT ( 'NONE',  ( 81.18398860626899705, 28.73617430169844056, 5.000000000000000000 ) ) ;
#58891=ORIENTED_EDGE ( 'NONE', *, *, #135884, .F. ) ;
#58893=ORIENTED_EDGE ( 'NONE', *, *, #52022, .T. ) ;
#58894=CARTESIAN_POINT ( 'NONE',  ( 13.49999999999991296, 6.052185695429103340, 5.000000000000000000 ) ) ;
#58895=PLANE ( 'NONE',  #8923 ) ;
#58896=VECTOR ( 'NONE', #106168, 1000.000000000000000 ) ;
#58899=VECTOR ( 'NONE', #111075, 1000.000000000000000 ) ;
#58900=LINE ( 'NONE', #100211, #143290 ) ;
#58901=ORIENTED_EDGE ( 'NONE', *, *, #13972, .T. ) ;
#58903=DIRECTION ( 'NONE',  ( 1.000000000000000000, 0.000000000000000000, 0.000000000000000000 ) ) ;
#58904=CARTESIAN_POINT ( 'NONE',  ( 63.18398860626900415, 28.73617430169831621, 5.000000000000000000 ) ) ;
#58905=DIRECTION ( 'NONE',  ( 0.7071067811865487940, 0.7071067811865463515, 0.000000000000000000 ) ) ;
#58906=CARTESIAN_POINT ( 'NONE',  ( 11.99999999999990585, -10.77435723561694836, -9.972017380717259627 ) ) ;
#58907=CARTESIAN_POINT ( 'NONE',  ( -3.511686059284292671, 6.759292476615660128, 16.35960578974470536 ) ) ;
#58908=LINE ( 'NONE', #124105, #97446 ) ;
#58909=VERTEX_POINT ( 'NONE', #53894 ) ;
#58910=ORIENTED_EDGE ( 'NONE', *, *, #93325, .F. ) ;
#58911=VERTEX_POINT ( 'NONE', #88652 ) ;
#58913=ORIENTED_EDGE ( 'NONE', *, *, #775, .F. ) ;
#58914=AXIS2_PLACEMENT_3D ( 'NONE', #78271, #100728, #123923 ) ;
#58915=EDGE_LOOP ( 'NONE', ( #122721, #63286, #83641 ) ) ;
#58916=AXIS2_PLACEMENT_3D ( 'NONE', #12522, #58962, #56800 ) ;
#58917=EDGE_LOOP ( 'NONE', ( #110006, #104417, #39666, #43362 ) ) ;
#58920=CARTESIAN_POINT ( 'NONE',  ( -8.994519915287490619, 28.92564299267944250, 4.000000000000000000 ) ) ;
#58921=ORIENTED_EDGE ( 'NONE', *, *, #117886, .T. ) ;
#58923=DIRECTION ( 'NONE',  ( -0.7071067811865487940, 0.7071067811865463515, -0.000000000000000000 ) ) ;
#58924=VECTOR ( 'NONE', #110304, 1000.000000000000000 ) ;
#58925=DIRECTION ( 'NONE',  ( -0.7071067811865486830, -0.7071067811865464625, 0.000000000000000000 ) ) ;
#58927=ORIENTED_EDGE ( 'NONE', *, *, #30269, .T. ) ;
#58928=ADVANCED_FACE ( 'NONE', ( #43701 ), #77770, .T. ) ;
#58929=DIRECTION ( 'NONE',  ( 0.6830127018922181881, 0.6830127018922202975, -0.2588190451025214056 ) ) ;
#58930=CARTESIAN_POINT ( 'NONE',  ( -30.77004279457771574, 21.73644205237998150, 5.000000000000000888 ) ) ;
#58933=DIRECTION ( 'NONE',  ( 0.6830127018922180770, -0.6830127018922202975, -0.2588190451025213501 ) ) ;
#58934=CARTESIAN_POINT ( 'NONE',  ( 19.49999999999986144, 9.431123077392085108, 4.000000000000000000 ) ) ;
#58935=CARTESIAN_POINT ( 'NONE',  ( 18.79289321881332242, 9.759292476615618384, 5.000000000000000000 ) ) ;
#58936=VECTOR ( 'NONE', #107974, 1000.000000000000000 ) ;
#58938=LINE ( 'NONE', #49469, #65318 ) ;
#58939=EDGE_CURVE ( 'NONE', #122403, #115805, #56040, .T. ) ;
#58941=LINE ( 'NONE', #94352, #90112 ) ;
#58942=EDGE_LOOP ( 'NONE', ( #27941, #121100, #112608, #30058 ) ) ;
#58945=ADVANCED_FACE ( 'NONE', ( #97330 ), #110355, .F. ) ;
#58946=ORIENTED_EDGE ( 'NONE', *, *, #58767, .T. ) ;
#58947=ORIENTED_EDGE ( 'NONE', *, *, #70265, .T. ) ;
#58949=EDGE_CURVE ( 'NONE', #138021, #66046, #21938, .T. ) ;
#58950=LINE ( 'NONE', #72672, #38525 ) ;
#58952=EDGE_CURVE ( 'NONE', #142812, #44722, #141595, .T. ) ;
#58955=LINE ( 'NONE', #57487, #113992 ) ;
#58958=VERTEX_POINT ( 'NONE', #119799 ) ;
#58959=EDGE_CURVE ( 'NONE', #39099, #60685, #66184, .T. ) ;
#58960=CARTESIAN_POINT ( 'NONE',  ( -14.92733143757284786, -1.141545485034857643, 4.000000000000000000 ) ) ;
#58961=ORIENTED_EDGE ( 'NONE', *, *, #88658, .T. ) ;
#58962=DIRECTION ( 'NONE',  ( 0.000000000000000000, 1.000000000000000000, 0.000000000000000000 ) ) ;
#58965=EDGE_CURVE ( 'NONE', #36583, #25072, #124117, .T. ) ;
#58967=VERTEX_POINT ( 'NONE', #79234 ) ;
#58968=ADVANCED_FACE ( 'NONE', ( #102391 ), #3720, .T. ) ;
#58969=VERTEX_POINT ( 'NONE', #92181 ) ;
#58970=CARTESIAN_POINT ( 'NONE',  ( -33.48921356237309510, -27.52281430457078670, 5.000000000000000000 ) ) ;
#58971=LINE ( 'NONE', #26985, #23035 ) ;
#58972=LINE ( 'NONE', #137197, #82467 ) ;
#58973=EDGE_CURVE ( 'NONE', #31906, #60720, #113953, .T. ) ;
#58975=DIRECTION ( 'NONE',  ( 0.7071067811865487940, 0.7071067811865463515, 0.000000000000000000 ) ) ;
#58976=ORIENTED_EDGE ( 'NONE', *, *, #51948, .T. ) ;
#58977=ORIENTED_EDGE ( 'NONE', *, *, #45029, .F. ) ;
#58978=DIRECTION ( 'NONE',  ( -0.7071067811865487940, 0.7071067811865463515, -0.000000000000000000 ) ) ;
#58979=ORIENTED_EDGE ( 'NONE', *, *, #114923, .T. ) ;
#58983=ORIENTED_EDGE ( 'NONE', *, *, #67622, .F. ) ;
#58984=CARTESIAN_POINT ( 'NONE',  ( 34.92499999999997584, 7.800094516027095359, 4.759050581649322709 ) ) ;
#58985=ADVANCED_FACE ( 'NONE', ( #78480 ), #67632, .F. ) ;
#58987=FACE_BOUND ( 'NONE', #71406, .T. ) ;
#58990=DIRECTION ( 'NONE',  ( -0.7071067811865486830, -0.7071067811865464625, 0.000000000000000000 ) ) ;
#58991=CARTESIAN_POINT ( 'NONE',  ( 34.92499999999998295, -20.33753812416077267, 4.000000000000000000 ) ) ;
#58992=CARTESIAN_POINT ( 'NONE',  ( 20.20710678118641468, 18.75929247661552068, 5.000000000000000000 ) ) ;
#58994=VECTOR ( 'NONE', #135812, 1000.000000000000114 ) ;
#58996=EDGE_CURVE ( 'NONE', #51865, #31605, #122675, .T. ) ;
#58998=VECTOR ( 'NONE', #26082, 1000.000000000000000 ) ;
#59001=ORIENTED_EDGE ( 'NONE', *, *, #4833, .F. ) ;
#59002=CARTESIAN_POINT ( 'NONE',  ( 66.18398860626901126, 28.73617430169833753, 5.000000000000000000 ) ) ;
#59003=VECTOR ( 'NONE', #57644, 1000.000000000000000 ) ;
#59004=EDGE_CURVE ( 'NONE', #3762, #118999, #25502, .T. ) ;
#59006=DIRECTION ( 'NONE',  ( -1.000000000000000000, 0.000000000000000000, -0.000000000000000000 ) ) ;
#59007=LINE ( 'NONE', #95670, #61204 ) ;
#59008=CARTESIAN_POINT ( 'NONE',  ( 11.51078643762690490, -27.52281430457047406, 5.000000000000000000 ) ) ;
#59009=VECTOR ( 'NONE', #128387, 999.9999999999998863 ) ;
#59010=EDGE_CURVE ( 'NONE', #75896, #54552, #69779, .T. ) ;
#59011=FACE_OUTER_BOUND ( 'NONE', #126267, .T. ) ;
#59012=CARTESIAN_POINT ( 'NONE',  ( 29.71998032010578328, 0.7592924766157173044, 14.27032725228015764 ) ) ;
#59013=PLANE ( 'NONE',  #35469 ) ;
#59014=CARTESIAN_POINT ( 'NONE',  ( -78.18398860626899705, 28.73617430169841924, 5.000000000000000000 ) ) ;
#59015=VERTEX_POINT ( 'NONE', #111824 ) ;
#59016=ORIENTED_EDGE ( 'NONE', *, *, #81909, .F. ) ;
#59018=CARTESIAN_POINT ( 'NONE',  ( 29.99451991528749417, 28.92564299267958816, 4.000000000000000000 ) ) ;
#59019=ORIENTED_EDGE ( 'NONE', *, *, #44182, .T. ) ;
#59021=EDGE_LOOP ( 'NONE', ( #120814, #143235, #136137, #139543 ) ) ;
#59022=EDGE_CURVE ( 'NONE', #12165, #59626, #79945, .T. ) ;
#59023=LINE ( 'NONE', #3818, #85507 ) ;
#59025=DIRECTION ( 'NONE',  ( 1.000000000000000000, 0.000000000000000000, 0.000000000000000000 ) ) ;
#59026=LINE ( 'NONE', #4515, #33108 ) ;
#59027=VECTOR ( 'NONE', #89073, 1000.000000000000000 ) ;
#59029=AXIS2_PLACEMENT_3D ( 'NONE', #31898, #88438, #143503 ) ;
#59030=CARTESIAN_POINT ( 'NONE',  ( 0.000000000000000000, 0.000000000000000000, 5.000000000000000000 ) ) ;
#59031=ORIENTED_EDGE ( 'NONE', *, *, #53776, .T. ) ;
#59032=AXIS2_PLACEMENT_3D ( 'NONE', #11290, #76620, #10591 ) ;
#59033=DIRECTION ( 'NONE',  ( -0.000000000000000000, 0.3543493200069152138, -0.9351131265310292928 ) ) ;
#59035=LINE ( 'NONE', #48117, #5750 ) ;
#59036=FACE_OUTER_BOUND ( 'NONE', #138299, .T. ) ;
#59037=VERTEX_POINT ( 'NONE', #113223 ) ;
#59038=VERTEX_POINT ( 'NONE', #137145 ) ;
#59039=CARTESIAN_POINT ( 'NONE',  ( -34.92500000000001137, 22.22500000000000142, 4.500000000000000888 ) ) ;
#59040=DIRECTION ( 'NONE',  ( -0.000000000000000000, 0.3543493200069153248, 0.9351131265310292928 ) ) ;
#59041=CARTESIAN_POINT ( 'NONE',  ( 26.99451991528749417, 28.92564299267956685, 4.000000000000000000 ) ) ;
#59042=ORIENTED_EDGE ( 'NONE', *, *, #41839, .F. ) ;
#59044=PLANE ( 'NONE',  #36345 ) ;
#59045=EDGE_CURVE ( 'NONE', #87113, #86807, #124830, .T. ) ;
#59047=CARTESIAN_POINT ( 'NONE',  ( -28.00193056682078918, -22.22500000000000142, 4.500000000000000888 ) ) ;
#59048=LINE ( 'NONE', #103893, #130107 ) ;
#59049=VERTEX_POINT ( 'NONE', #59602 ) ;
#59050=CARTESIAN_POINT ( 'NONE',  ( -13.49999999999991118, 14.14708470758590053, -0.5283514160166246088 ) ) ;
#59051=DIRECTION ( 'NONE',  ( 0.3543493200069162685, -0.000000000000000000, -0.9351131265310288487 ) ) ;
#59053=DIRECTION ( 'NONE',  ( 1.000000000000000000, 0.000000000000000000, 0.000000000000000000 ) ) ;
#59056=VERTEX_POINT ( 'NONE', #2297 ) ;
#59057=CARTESIAN_POINT ( 'NONE',  ( 26.67183060077629264, -3.740707523384234623, 4.000000000000000000 ) ) ;
#59061=DIRECTION ( 'NONE',  ( 0.7071067811865486830, -0.7071067811865464625, -0.000000000000000000 ) ) ;
#59062=LINE ( 'NONE', #69188, #127033 ) ;
#59063=DIRECTION ( 'NONE',  ( -0.7071067811865487940, 0.7071067811865463515, -0.000000000000000000 ) ) ;
#59064=ORIENTED_EDGE ( 'NONE', *, *, #126323, .F. ) ;
#59066=CARTESIAN_POINT ( 'NONE',  ( 34.92499999999998295, 9.856123077392316745, 4.000000000000000000 ) ) ;
#59067=FACE_OUTER_BOUND ( 'NONE', #117899, .T. ) ;
#59069=EDGE_CURVE ( 'NONE', #42800, #140795, #123441, .T. ) ;
#59070=VECTOR ( 'NONE', #135306, 1000.000000000000227 ) ;
#59071=CARTESIAN_POINT ( 'NONE',  ( -30.29974487139158867, -27.71228299555227537, 4.000000000000000000 ) ) ;
#59072=DIRECTION ( 'NONE',  ( 1.000000000000000000, 0.000000000000000000, 0.000000000000000000 ) ) ;
#59074=CARTESIAN_POINT ( 'NONE',  ( -11.81601139373100651, 28.73617430169779041, 5.000000000000000000 ) ) ;
#59075=ORIENTED_EDGE ( 'NONE', *, *, #63784, .T. ) ;
#59076=DIRECTION ( 'NONE',  ( -0.7071067811865486830, -0.7071067811865464625, 0.000000000000000000 ) ) ;
#59077=LINE ( 'NONE', #81531, #15991 ) ;
#59078=PLANE ( 'NONE',  #106714 ) ;
#59079=DIRECTION ( 'NONE',  ( -0.000000000000000000, 0.000000000000000000, 1.000000000000000000 ) ) ;
#59082=ORIENTED_EDGE ( 'NONE', *, *, #100926, .F. ) ;
#59083=CARTESIAN_POINT ( 'NONE',  ( -9.758600742197899081, 21.72500000000000853, 5.000000000000000000 ) ) ;
#59084=LINE ( 'NONE', #69965, #51492 ) ;
#59086=CARTESIAN_POINT ( 'NONE',  ( -15.18398860626900237, 28.73617430169797871, 5.000000000000000000 ) ) ;
#59087=CARTESIAN_POINT ( 'NONE',  ( 34.42499999999998295, -18.02281430457042433, 5.000000000000000000 ) ) ;
#59089=VECTOR ( 'NONE', #57845, 1000.000000000000000 ) ;
#59090=EDGE_CURVE ( 'NONE', #96272, #57196, #34993, .T. ) ;
#59091=DIRECTION ( 'NONE',  ( -0.000000000000000000, 0.3543493200069153248, 0.9351131265310292928 ) ) ;
#59092=VERTEX_POINT ( 'NONE', #4404 ) ;
#59093=( BOUNDED_CURVE ( )  B_SPLINE_CURVE ( 3, ( #37217, #82184, #82881, #140117 ),
 .UNSPECIFIED., .F., .T. ) 
 B_SPLINE_CURVE_WITH_KNOTS ( ( 4, 4 ),
 ( 1.864375635226923844, 1.933014472006567175 ),
 .UNSPECIFIED. ) 
 CURVE ( )  GEOMETRIC_REPRESENTATION_ITEM ( )  RATIONAL_B_SPLINE_CURVE ( ( 1.000000000000000000, 0.9996074310407760954, 0.9996074310407760954, 1.000000000000000000 ) ) 
 REPRESENTATION_ITEM ( '' )  );
#59095=CARTESIAN_POINT ( 'NONE',  ( 15.60486233187511473, 21.75929247661549226, 21.32995629748182864 ) ) ;
#59097=VECTOR ( 'NONE', #71198, 1000.000000000000227 ) ;
#59098=LINE ( 'NONE', #50326, #141136 ) ;
#59099=CARTESIAN_POINT ( 'NONE',  ( 16.49999999999988987, 22.08746187583901843, 4.000000000000000000 ) ) ;
#59102=ADVANCED_FACE ( 'NONE', ( #135715 ), #36399, .F. ) ;
#59103=FACE_OUTER_BOUND ( 'NONE', #74575, .T. ) ;
#59104=AXIS2_PLACEMENT_3D ( 'NONE', #64377, #129617, #86855 ) ;
#59107=CARTESIAN_POINT ( 'NONE',  ( -18.63311396761903538, -2.779424156541560276, 4.000000000000000000 ) ) ;
#59111=CARTESIAN_POINT ( 'NONE',  ( -29.99999999999979039, -16.60178936734451582, 0.8616154019346804471 ) ) ;
#59112=DIRECTION ( 'NONE',  ( -0.6830127018922181881, 0.6830127018922202975, -0.2588190451025214056 ) ) ;
#59113=EDGE_CURVE ( 'NONE', #37315, #119727, #39266, .T. ) ;
#59114=PLANE ( 'NONE',  #69553 ) ;
#59115=ADVANCED_FACE ( 'NONE', ( #29782 ), #51574, .T. ) ;
#59116=CARTESIAN_POINT ( 'NONE',  ( 32.99451991528749062, 28.92564299267960948, 4.000000000000000000 ) ) ;
#59117=CARTESIAN_POINT ( 'NONE',  ( 3.183988606268992161, 28.73617430169789699, 5.000000000000000000 ) ) ;
#59118=VERTEX_POINT ( 'NONE', #50139 ) ;
#59119=CARTESIAN_POINT ( 'NONE',  ( -24.00548008471250938, 28.92564299267921513, 4.000000000000000000 ) ) ;
#59120=CARTESIAN_POINT ( 'NONE',  ( 23.99999999999983302, 15.45873954670187622, -0.03131636524299555302 ) ) ;
#59121=DIRECTION ( 'NONE',  ( -0.7071067811865486830, -0.7071067811865464625, -0.000000000000000000 ) ) ;
#59123=EDGE_CURVE ( 'NONE', #137944, #39127, #74027, .T. ) ;
#59124=VECTOR ( 'NONE', #92030, 999.9999999999998863 ) ;
#59125=ORIENTED_EDGE ( 'NONE', *, *, #66035, .F. ) ;
#59126=VECTOR ( 'NONE', #80753, 1000.000000000000000 ) ;
#59128=EDGE_LOOP ( 'NONE', ( #30748, #120079, #122598, #55232 ) ) ;
#59129=AXIS2_PLACEMENT_3D ( 'NONE', #107453, #137966, #8120 ) ;
#59130=LINE ( 'NONE', #103279, #114698 ) ;
#59131=DIRECTION ( 'NONE',  ( -0.6830127018922181881, 0.6830127018922202975, -0.2588190451025214056 ) ) ;
#59132=DIRECTION ( 'NONE',  ( -0.6830127018922180770, -0.6830127018922204085, -0.2588190451025213501 ) ) ;
#59135=ORIENTED_EDGE ( 'NONE', *, *, #14444, .T. ) ;
#59136=EDGE_CURVE ( 'NONE', #25035, #56060, #49452, .T. ) ;
#59137=CARTESIAN_POINT ( 'NONE',  ( -20.46326412755669111, -2.625232532701756494, 4.661243073242806290 ) ) ;
#59138=DIRECTION ( 'NONE',  ( 0.7071067811865486830, -0.7071067811865464625, -0.000000000000000000 ) ) ;
#59139=ORIENTED_EDGE ( 'NONE', *, *, #28249, .F. ) ;
#59142=CARTESIAN_POINT ( 'NONE',  ( -23.99451991528749062, 28.92564299267954908, 4.000000000000000000 ) ) ;
#59143=EDGE_CURVE ( 'NONE', #36339, #76243, #40689, .T. ) ;
#59144=CARTESIAN_POINT ( 'NONE',  ( 0.000000000000000000, 0.000000000000000000, 5.000000000000000000 ) ) ;
#59145=ORIENTED_EDGE ( 'NONE', *, *, #107461, .F. ) ;
#59146=FACE_BOUND ( 'NONE', #98317, .T. ) ;
#59147=PLANE ( 'NONE',  #73348 ) ;
#59148=PLANE ( 'NONE',  #118415 ) ;
#59149=PLANE ( 'NONE',  #82968 ) ;
#59150=DIRECTION ( 'NONE',  ( 1.000000000000000000, 0.000000000000000000, 0.000000000000000000 ) ) ;
#59153=( BOUNDED_CURVE ( )  B_SPLINE_CURVE ( 3, ( #62954, #42632, #107129, #140474 ),
 .UNSPECIFIED., .F., .T. ) 
 B_SPLINE_CURVE_WITH_KNOTS ( ( 4, 4 ),
 ( 2.779374508378133601, 4.199602562396794525 ),
 .UNSPECIFIED. ) 
 CURVE ( )  GEOMETRIC_REPRESENTATION_ITEM ( )  RATIONAL_B_SPLINE_CURVE ( ( 1.000000000000000000, 0.8388583629366721528, 0.8388583629366721528, 1.000000000000000000 ) ) 
 REPRESENTATION_ITEM ( '' )  );
#59154=ADVANCED_FACE ( 'NONE', ( #128413 ), #116083, .F. ) ;
#59155=ORIENTED_EDGE ( 'NONE', *, *, #84024, .F. ) ;
#59159=DIRECTION ( 'NONE',  ( 0.7071067811865486830, -0.7071067811865464625, -0.000000000000000000 ) ) ;
#59160=DIRECTION ( 'NONE',  ( 0.7071067811865487940, 0.7071067811865463515, 0.000000000000000000 ) ) ;
#59162=LINE ( 'NONE', #127970, #47139 ) ;
#59164=DIRECTION ( 'NONE',  ( -0.000000000000000000, 0.3543493200069153248, 0.9351131265310292928 ) ) ;
#59165=CARTESIAN_POINT ( 'NONE',  ( 0.000000000000000000, 0.000000000000000000, 5.000000000000000000 ) ) ;
#59166=EDGE_CURVE ( 'NONE', #131471, #17257, #82766, .T. ) ;
#59168=LINE ( 'NONE', #113485, #103569 ) ;
#59169=CARTESIAN_POINT ( 'NONE',  ( -17.99999999999986855, -7.447814304570745669, 5.000000000000000000 ) ) ;
#59170=DIRECTION ( 'NONE',  ( -0.3543493200069162685, -0.000000000000000000, -0.9351131265310288487 ) ) ;
#59172=ORIENTED_EDGE ( 'NONE', *, *, #36600, .T. ) ;
#59173=LINE ( 'NONE', #25777, #119050 ) ;
#59174=DIRECTION ( 'NONE',  ( 0.7071067811865486830, -0.7071067811865464625, -0.000000000000000000 ) ) ;
#59175=ORIENTED_EDGE ( 'NONE', *, *, #131812, .T. ) ;
#59176=VERTEX_POINT ( 'NONE', #107355 ) ;
#59178=ORIENTED_EDGE ( 'NONE', *, *, #118593, .T. ) ;
#59180=VERTEX_POINT ( 'NONE', #138572 ) ;
#59181=VECTOR ( 'NONE', #34466, 1000.000000000000000 ) ;
#59184=ORIENTED_EDGE ( 'NONE', *, *, #57634, .F. ) ;
#59186=ADVANCED_FACE ( 'NONE', ( #18918 ), #63184, .T. ) ;
#59187=CARTESIAN_POINT ( 'NONE',  ( -5.999999999999956479, -13.97847968911261063, -0.1324546996126930165 ) ) ;
#59188=ORIENTED_EDGE ( 'NONE', *, *, #68513, .F. ) ;
#59190=CARTESIAN_POINT ( 'NONE',  ( 0.000000000000000000, 0.000000000000000000, 5.000000000000000000 ) ) ;
#59191=ORIENTED_EDGE ( 'NONE', *, *, #138942, .T. ) ;
#59192=ORIENTED_EDGE ( 'NONE', *, *, #95469, .F. ) ;
#59193=DIRECTION ( 'NONE',  ( 1.000000000000000000, 0.000000000000000000, 0.000000000000000000 ) ) ;
#59194=DIRECTION ( 'NONE',  ( 0.000000000000000000, 0.3543493200069153248, 0.9351131265310291818 ) ) ;
#59196=ORIENTED_EDGE ( 'NONE', *, *, #55094, .T. ) ;
#59198=EDGE_LOOP ( 'NONE', ( #119901, #83470, #32754 ) ) ;
#59199=AXIS2_PLACEMENT_3D ( 'NONE', #67239, #56406, #112867 ) ;
#59201=ORIENTED_EDGE ( 'NONE', *, *, #90169, .F. ) ;
#59202=EDGE_LOOP ( 'NONE', ( #7629, #22552, #98370, #84788 ) ) ;
#59203=ORIENTED_EDGE ( 'NONE', *, *, #66495, .T. ) ;
#59205=CARTESIAN_POINT ( 'NONE',  ( -16.49999999999988276, 15.05218569542901186, 5.000000000000000000 ) ) ;
#59208=DIRECTION ( 'NONE',  ( -0.7071067811865486830, -0.7071067811865464625, 0.000000000000000000 ) ) ;
#59209=EDGE_CURVE ( 'NONE', #79521, #42427, #82082, .T. ) ;
#59210=CARTESIAN_POINT ( 'NONE',  ( -32.29289321881323360, -9.740707523384186217, 5.000000000000000000 ) ) ;
#59211=ORIENTED_EDGE ( 'NONE', *, *, #30816, .T. ) ;
#59212=LINE ( 'NONE', #100544, #88995 ) ;
#59213=VECTOR ( 'NONE', #92737, 1000.000000000000000 ) ;
#59215=CARTESIAN_POINT ( 'NONE',  ( -3.722814304570581712, -21.72499999999999432, 5.000000000000000000 ) ) ;
#59216=VECTOR ( 'NONE', #59796, 999.9999999999998863 ) ;
#59217=DIRECTION ( 'NONE',  ( -0.000000000000000000, 0.000000000000000000, 1.000000000000000000 ) ) ;
#59218=VECTOR ( 'NONE', #21323, 1000.000000000000000 ) ;
#59219=EDGE_CURVE ( 'NONE', #47367, #83534, #52262, .T. ) ;
#59221=EDGE_LOOP ( 'NONE', ( #789, #36834, #68825, #47706 ) ) ;
#59222=VERTEX_POINT ( 'NONE', #26939 ) ;
#59223=ORIENTED_EDGE ( 'NONE', *, *, #68956, .T. ) ;
#59224=CARTESIAN_POINT ( 'NONE',  ( 10.17183060077639922, -14.24070752338414003, 4.000000000000000000 ) ) ;
#59225=CARTESIAN_POINT ( 'NONE',  ( 39.18398860626899705, 28.73617430169814568, 5.000000000000000000 ) ) ;
#59227=CARTESIAN_POINT ( 'NONE',  ( 27.48921356237309155, -27.52281430457074762, 5.000000000000000000 ) ) ;
#59228=VECTOR ( 'NONE', #60675, 999.9999999999998863 ) ;
#59229=CARTESIAN_POINT ( 'NONE',  ( 0.000000000000000000, 0.000000000000000000, 5.000000000000000000 ) ) ;
#59230=LINE ( 'NONE', #136732, #6481 ) ;
#59231=LINE ( 'NONE', #80254, #84836 ) ;
#59232=ADVANCED_FACE ( 'NONE', ( #71187 ), #115335, .F. ) ;
#59234=FACE_OUTER_BOUND ( 'NONE', #120880, .T. ) ;
#59236=CARTESIAN_POINT ( 'NONE',  ( -25.82816939922335209, 18.75929247661552068, 4.000000000000000000 ) ) ;
#59237=LINE ( 'NONE', #38873, #97430 ) ;
#59238=ORIENTED_EDGE ( 'NONE', *, *, #56790, .T. ) ;
#59240=ORIENTED_EDGE ( 'NONE', *, *, #21907, .F. ) ;
#59241=LINE ( 'NONE', #27266, #22826 ) ;
#59243=ORIENTED_EDGE ( 'NONE', *, *, #94829, .F. ) ;
#59244=DIRECTION ( 'NONE',  ( -0.000000000000000000, 0.000000000000000000, 1.000000000000000000 ) ) ;
#59245=CARTESIAN_POINT ( 'NONE',  ( 30.48921356237309510, -27.52281430457076894, 5.000000000000000000 ) ) ;
#59246=ORIENTED_EDGE ( 'NONE', *, *, #59022, .T. ) ;
#59247=DIRECTION ( 'NONE',  ( 1.000000000000000000, 0.000000000000000000, 0.000000000000000000 ) ) ;
#59250=ORIENTED_EDGE ( 'NONE', *, *, #13389, .F. ) ;
#59251=CARTESIAN_POINT ( 'NONE',  ( 18.81349135397627492, -15.74070752338412760, 8.904080028138896097 ) ) ;
#59254=EDGE_CURVE ( 'NONE', #15997, #33874, #95039, .T. ) ;
#59255=CARTESIAN_POINT ( 'NONE',  ( -0.2997448713915885632, -27.71228299555206220, 4.000000000000000000 ) ) ;
#59256=VERTEX_POINT ( 'NONE', #10178 ) ;
#59258=DIRECTION ( 'NONE',  ( -0.3543493200069162685, -0.000000000000000000, -0.9351131265310288487 ) ) ;
#59259=EDGE_CURVE ( 'NONE', #69474, #25047, #87042, .T. ) ;
#59260=DIRECTION ( 'NONE',  ( 0.7071067811865487940, 0.7071067811865463515, -0.000000000000000000 ) ) ;
#59262=LINE ( 'NONE', #101295, #114913 ) ;
#59264=EDGE_CURVE ( 'NONE', #89344, #25946, #42132, .T. ) ;
#59265=EDGE_CURVE ( 'NONE', #26035, #79450, #129827, .T. ) ;
#59266=FACE_OUTER_BOUND ( 'NONE', #129146, .T. ) ;
#59267=ORIENTED_EDGE ( 'NONE', *, *, #33506, .F. ) ;
#59269=FACE_OUTER_BOUND ( 'NONE', #48672, .T. ) ;
#59271=LINE ( 'NONE', #93286, #79372 ) ;
#59273=ORIENTED_EDGE ( 'NONE', *, *, #96828, .F. ) ;
#59275=CARTESIAN_POINT ( 'NONE',  ( -15.18398860626900237, 28.73617430169797871, 5.000000000000000000 ) ) ;
#59276=EDGE_CURVE ( 'NONE', #84184, #64792, #131258, .T. ) ;
#59277=ORIENTED_EDGE ( 'NONE', *, *, #96277, .T. ) ;
#59278=DIRECTION ( 'NONE',  ( -0.6830127018922181881, 0.6830127018922202975, -0.2588190451025214056 ) ) ;
#59279=EDGE_CURVE ( 'NONE', #24662, #109601, #132726, .T. ) ;
#59280=DIRECTION ( 'NONE',  ( -0.6830127018922180770, -0.6830127018922204085, -0.2588190451025213501 ) ) ;
#59281=CARTESIAN_POINT ( 'NONE',  ( 16.49999999999988987, 16.77039438581780573, 0.4657186855307349771 ) ) ;
#59283=LINE ( 'NONE', #92558, #46076 ) ;
#59284=CARTESIAN_POINT ( 'NONE',  ( -34.92500000000001137, 13.80009451602706783, 4.759050581649336920 ) ) ;
#59285=CARTESIAN_POINT ( 'NONE',  ( 0.000000000000000000, 0.000000000000000000, 5.000000000000000000 ) ) ;
#59287=ORIENTED_EDGE ( 'NONE', *, *, #8982, .T. ) ;
#59288=VECTOR ( 'NONE', #39116, 1000.000000000000000 ) ;
#59289=VERTEX_POINT ( 'NONE', #31946 ) ;
#59290=EDGE_LOOP ( 'NONE', ( #5243, #74879, #104523, #15777 ) ) ;
#59292=ORIENTED_EDGE ( 'NONE', *, *, #138047, .T. ) ;
#59293=EDGE_CURVE ( 'NONE', #89747, #107875, #30532, .T. ) ;
#59294=VECTOR ( 'NONE', #73199, 999.9999999999998863 ) ;
#59296=DIRECTION ( 'NONE',  ( 0.6830127018922180770, -0.6830127018922204085, -0.2588190451025213501 ) ) ;
#59297=DIRECTION ( 'NONE',  ( -0.7071067811865486830, -0.7071067811865464625, 0.000000000000000000 ) ) ;
#59298=DIRECTION ( 'NONE',  ( -0.6830127018922181881, 0.6830127018922202975, -0.2588190451025214056 ) ) ;
#59299=VERTEX_POINT ( 'NONE', #21053 ) ;
#59301=DIRECTION ( 'NONE',  ( 0.3543493200069162685, -0.000000000000000000, -0.9351131265310288487 ) ) ;
#59304=AXIS2_PLACEMENT_3D ( 'NONE', #101100, #77945, #22792 ) ;
#59305=LINE ( 'NONE', #112927, #136884 ) ;
#59306=CARTESIAN_POINT ( 'NONE',  ( -9.328169399223463998, -18.74070752338408852, 4.000000000000000000 ) ) ;
#59308=DIRECTION ( 'NONE',  ( 0.6830127018922181881, 0.6830127018922202975, -0.2588190451025214056 ) ) ;
#59309=ORIENTED_EDGE ( 'NONE', *, *, #19568, .F. ) ;
#59310=ORIENTED_EDGE ( 'NONE', *, *, #103845, .F. ) ;
#59311=DIRECTION ( 'NONE',  ( -0.6830127018922180770, -0.6830127018922204085, -0.2588190451025213501 ) ) ;
#59315=ADVANCED_FACE ( 'NONE', ( #66719 ), #119632, .F. ) ;
#59318=DIRECTION ( 'NONE',  ( -0.7071067811865487940, 0.7071067811865463515, 0.000000000000000000 ) ) ;
#59319=DIRECTION ( 'NONE',  ( -0.7071067811865486830, -0.7071067811865464625, 0.000000000000000000 ) ) ;
#59320=EDGE_CURVE ( 'NONE', #103659, #114199, #33415, .T. ) ;
#59322=VERTEX_POINT ( 'NONE', #131988 ) ;
#59324=AXIS2_PLACEMENT_3D ( 'NONE', #3573, #4247, #47866 ) ;
#59326=ORIENTED_EDGE ( 'NONE', *, *, #23702, .F. ) ;
#59327=AXIS2_PLACEMENT_3D ( 'NONE', #29767, #72632, #95754 ) ;
#59328=EDGE_CURVE ( 'NONE', #89130, #81231, #128176, .T. ) ;
#59329=CARTESIAN_POINT ( 'NONE',  ( -10.17183060077640100, -5.240707523384232402, 4.000000000000000000 ) ) ;
#59330=ORIENTED_EDGE ( 'NONE', *, *, #38086, .F. ) ;
#59332=DIRECTION ( 'NONE',  ( 0.6830127018922181881, 0.6830127018922202975, -0.2588190451025214056 ) ) ;
#59333=CARTESIAN_POINT ( 'NONE',  ( 69.18398860626899705, 28.73617430169835529, 5.000000000000000000 ) ) ;
#59334=PLANE ( 'NONE',  #56103 ) ;
#59335=ORIENTED_EDGE ( 'NONE', *, *, #18785, .F. ) ;
#59336=LINE ( 'NONE', #4128, #44920 ) ;
#59337=DIRECTION ( 'NONE',  ( 0.3543493200069162685, -0.000000000000000000, -0.9351131265310288487 ) ) ;
#59339=CARTESIAN_POINT ( 'NONE',  ( -32.27718569542918203, -21.72500000000000142, 5.000000000000000000 ) ) ;
#59340=EDGE_LOOP ( 'NONE', ( #140894, #64270, #44767, #64816 ) ) ;
#59341=ORIENTED_EDGE ( 'NONE', *, *, #97701, .T. ) ;
#59343=ORIENTED_EDGE ( 'NONE', *, *, #16515, .F. ) ;
#59346=EDGE_LOOP ( 'NONE', ( #44309, #134765, #23864, #25002 ) ) ;
#59347=DIRECTION ( 'NONE',  ( -0.7071067811865486830, -0.7071067811865464625, 0.000000000000000000 ) ) ;
#59348=DIRECTION ( 'NONE',  ( -0.7071067811865486830, -0.7071067811865464625, 0.000000000000000000 ) ) ;
#59350=CARTESIAN_POINT ( 'NONE',  ( 24.18398860626899705, 28.73617430169804265, 5.000000000000000000 ) ) ;
#59352=DIRECTION ( 'NONE',  ( -0.000000000000000000, 0.3543493200069153248, 0.9351131265310292928 ) ) ;
#59354=VECTOR ( 'NONE', #73679, 1000.000000000000000 ) ;
#59355=CARTESIAN_POINT ( 'NONE',  ( -36.18398860626899705, 28.73617430169812437, 5.000000000000000000 ) ) ;
#59359=DIRECTION ( 'NONE',  ( -1.000000000000000000, 0.000000000000000000, -0.000000000000000000 ) ) ;
#59360=EDGE_LOOP ( 'NONE', ( #135284, #38628, #31430, #89774 ) ) ;
#59361=ORIENTED_EDGE ( 'NONE', *, *, #58790, .F. ) ;
#59362=VECTOR ( 'NONE', #95929, 1000.000000000000227 ) ;
#59364=EDGE_LOOP ( 'NONE', ( #90746, #19587, #139231, #49238 ) ) ;
#59366=PLANE ( 'NONE',  #7402 ) ;
#59367=LINE ( 'NONE', #70267, #121890 ) ;
#59368=EDGE_CURVE ( 'NONE', #18045, #9940, #118943, .T. ) ;
#59369=CARTESIAN_POINT ( 'NONE',  ( -5.540161610502567058, 18.75929247661553489, 8.305906642995470435 ) ) ;
#59371=ORIENTED_EDGE ( 'NONE', *, *, #29296, .F. ) ;
#59373=CARTESIAN_POINT ( 'NONE',  ( -20.99451991528748707, 28.92564299267952777, 4.000000000000000000 ) ) ;
#59374=VERTEX_POINT ( 'NONE', #97921 ) ;
#59375=CARTESIAN_POINT ( 'NONE',  ( -29.99999999999978684, -10.06887692260770883, 4.000000000000000000 ) ) ;
#59376=EDGE_CURVE ( 'NONE', #88631, #100364, #110897, .T. ) ;
#59377=VECTOR ( 'NONE', #50399, 1000.000000000000227 ) ;
#59380=VECTOR ( 'NONE', #53388, 999.9999999999998863 ) ;
#59382=LINE ( 'NONE', #103537, #69833 ) ;
#59383=ORIENTED_EDGE ( 'NONE', *, *, #23332, .F. ) ;
#59384=ORIENTED_EDGE ( 'NONE', *, *, #139127, .F. ) ;
#59385=ORIENTED_EDGE ( 'NONE', *, *, #94440, .T. ) ;
#59387=DIRECTION ( 'NONE',  ( 0.3543493200069162685, -0.000000000000000000, -0.9351131265310288487 ) ) ;
#59388=DIRECTION ( 'NONE',  ( -0.3543493200069162685, -0.000000000000000000, -0.9351131265310288487 ) ) ;
#59390=VERTEX_POINT ( 'NONE', #65320 ) ;
#59391=PLANE ( 'NONE',  #76355 ) ;
#59392=DIRECTION ( 'NONE',  ( 0.7071067811865486830, -0.7071067811865464625, -0.000000000000000000 ) ) ;
#59393=EDGE_CURVE ( 'NONE', #98666, #125641, #109504, .T. ) ;
#59395=AXIS2_PLACEMENT_3D ( 'NONE', #71602, #29494, #115055 ) ;
#59396=LINE ( 'NONE', #138353, #16472 ) ;
#59397=DIRECTION ( 'NONE',  ( -0.7071067811865486830, 0.7071067811865464625, 0.000000000000000000 ) ) ;
#59398=ORIENTED_EDGE ( 'NONE', *, *, #42689, .T. ) ;
#59399=DIRECTION ( 'NONE',  ( -0.3543493200069162685, -0.000000000000000000, -0.9351131265310288487 ) ) ;
#59400=EDGE_CURVE ( 'NONE', #103174, #127004, #55866, .T. ) ;
#59401=DIRECTION ( 'NONE',  ( 0.7071067811865487940, 0.7071067811865463515, 0.000000000000000000 ) ) ;
#59402=ORIENTED_EDGE ( 'NONE', *, *, #92753, .T. ) ;
#59404=ORIENTED_EDGE ( 'NONE', *, *, #133646, .T. ) ;
#59406=ORIENTED_EDGE ( 'NONE', *, *, #142880, .F. ) ;
#59407=DIRECTION ( 'NONE',  ( 0.7071067811865486830, -0.7071067811865464625, -0.000000000000000000 ) ) ;
#59409=DIRECTION ( 'NONE',  ( -0.7071067811865486830, -0.7071067811865464625, -0.000000000000000000 ) ) ;
#59410=EDGE_CURVE ( 'NONE', #133459, #124676, #15162, .T. ) ;
#59412=CARTESIAN_POINT ( 'NONE',  ( -8.510786437626906675, -27.52281430457049183, 5.000000000000000000 ) ) ;
#59415=CARTESIAN_POINT ( 'NONE',  ( 39.29974487139159578, -27.71228299555233576, 4.000000000000000000 ) ) ;
#59416=CARTESIAN_POINT ( 'NONE',  ( -7.499999999999951150, 9.431123077392088661, 4.000000000000000000 ) ) ;
#59417=VECTOR ( 'NONE', #29820, 999.9999999999998863 ) ;
#59419=DIRECTION ( 'NONE',  ( -0.7071067811865486830, -0.7071067811865464625, -0.000000000000000000 ) ) ;
#59420=DIRECTION ( 'NONE',  ( 0.7071067811865487940, 0.7071067811865463515, -0.000000000000000000 ) ) ;
#59421=PLANE ( 'NONE',  #19043 ) ;
#59422=DIRECTION ( 'NONE',  ( -0.7071067811865487940, 0.7071067811865463515, 0.000000000000000000 ) ) ;
#59423=EDGE_CURVE ( 'NONE', #123892, #4072, #67461, .T. ) ;
#59424=CARTESIAN_POINT ( 'NONE',  ( -0.7071067811865363595, -9.740707523384179112, 5.000000000000000000 ) ) ;
#59426=DIRECTION ( 'NONE',  ( -0.000000000000000000, 0.000000000000000000, 1.000000000000000000 ) ) ;
#59427=CARTESIAN_POINT ( 'NONE',  ( 13.17183060077638324, 18.75929247661553134, 4.000000000000000000 ) ) ;
#59428=VECTOR ( 'NONE', #134848, 1000.000000000000000 ) ;
#59430=FACE_OUTER_BOUND ( 'NONE', #37364, .T. ) ;
#59431=ORIENTED_EDGE ( 'NONE', *, *, #67320, .T. ) ;
#59432=EDGE_CURVE ( 'NONE', #46912, #25963, #2871, .T. ) ;
#59433=EDGE_LOOP ( 'NONE', ( #25201, #71750, #842, #35208 ) ) ;
#59434=EDGE_CURVE ( 'NONE', #57383, #34999, #34105, .T. ) ;
#59436=ORIENTED_EDGE ( 'NONE', *, *, #77385, .F. ) ;
#59437=VERTEX_POINT ( 'NONE', #78314 ) ;
#59439=FACE_OUTER_BOUND ( 'NONE', #4421, .T. ) ;
#59440=ORIENTED_EDGE ( 'NONE', *, *, #66847, .T. ) ;
#59441=DIRECTION ( 'NONE',  ( 1.000000000000000000, 0.000000000000000000, 0.000000000000000000 ) ) ;
#59443=CARTESIAN_POINT ( 'NONE',  ( 62.99451991528749772, 28.92564299267982264, 4.000000000000000000 ) ) ;
#59444=LINE ( 'NONE', #36933, #58065 ) ;
#59447=CARTESIAN_POINT ( 'NONE',  ( -23.99999999999983302, 17.96639925780207747, 5.000000000000000000 ) ) ;
#59448=FACE_OUTER_BOUND ( 'NONE', #19170, .T. ) ;
#59449=DIRECTION ( 'NONE',  ( -0.6830127018922180770, -0.6830127018922204085, -0.2588190451025213501 ) ) ;
#59450=DIRECTION ( 'NONE',  ( -0.7071067811865486830, 0.7071067811865464625, 0.000000000000000000 ) ) ;
#59451=CARTESIAN_POINT ( 'NONE',  ( 24.97566027651206610, 3.896288752498338948, 4.156157854036514721 ) ) ;
#59452=DIRECTION ( 'NONE',  ( -0.7071067811865487940, 0.7071067811865463515, 0.000000000000000000 ) ) ;
#59453=PLANE ( 'NONE',  #61494 ) ;
#59454=ORIENTED_EDGE ( 'NONE', *, *, #142426, .F. ) ;
#59455=ORIENTED_EDGE ( 'NONE', *, *, #9422, .F. ) ;
#59457=ORIENTED_EDGE ( 'NONE', *, *, #12983, .F. ) ;
#59458=EDGE_CURVE ( 'NONE', #126942, #106637, #123967, .T. ) ;
#59459=CARTESIAN_POINT ( 'NONE',  ( 26.67183060077628909, 20.25929247661551358, 4.000000000000000000 ) ) ;
#59460=AXIS2_PLACEMENT_3D ( 'NONE', #123285, #113807, #23956 ) ;
#59462=ORIENTED_EDGE ( 'NONE', *, *, #20911, .T. ) ;
#59463=ADVANCED_FACE ( 'NONE', ( #122502 ), #124661, .T. ) ;
#59464=DIRECTION ( 'NONE',  ( -0.7071067811865486830, -0.7071067811865463515, 0.000000000000000000 ) ) ;
#59467=ORIENTED_EDGE ( 'NONE', *, *, #31553, .T. ) ;
#59468=VERTEX_POINT ( 'NONE', #24629 ) ;
#59469=CARTESIAN_POINT ( 'NONE',  ( -11.81601139373100651, 28.73617430169779041, 5.000000000000000000 ) ) ;
#59470=AXIS2_PLACEMENT_3D ( 'NONE', #118204, #63875, #8019 ) ;
#59472=DIRECTION ( 'NONE',  ( -0.7071067811865486830, -0.7071067811865464625, 0.000000000000000000 ) ) ;
#59473=EDGE_LOOP ( 'NONE', ( #59860, #83475, #1552, #4121 ) ) ;
#59475=VECTOR ( 'NONE', #140575, 1000.000000000000000 ) ;
#59476=ORIENTED_EDGE ( 'NONE', *, *, #58758, .T. ) ;
#59477=CARTESIAN_POINT ( 'NONE',  ( -24.75149461641275295, 4.949500604449031727, 4.299609778361313417 ) ) ;
#59479=EDGE_CURVE ( 'NONE', #48159, #42968, #81177, .T. ) ;
#59481=VERTEX_POINT ( 'NONE', #112368 ) ;
#59482=VECTOR ( 'NONE', #106135, 1000.000000000000000 ) ;
#59483=VERTEX_POINT ( 'NONE', #36929 ) ;
#59484=CARTESIAN_POINT ( 'NONE',  ( -32.99451991528749062, 28.92564299267960948, 4.000000000000000000 ) ) ;
#59485=EDGE_LOOP ( 'NONE', ( #4706, #19640, #7650 ) ) ;
#59487=FACE_OUTER_BOUND ( 'NONE', #34858, .T. ) ;
#59488=CARTESIAN_POINT ( 'NONE',  ( 27.48921356237309155, -27.52281430457074762, 5.000000000000000000 ) ) ;
#59489=VERTEX_POINT ( 'NONE', #58753 ) ;
#59490=DIRECTION ( 'NONE',  ( 0.7071067811865487940, 0.7071067811865463515, 0.000000000000000000 ) ) ;
#59491=DIRECTION ( 'NONE',  ( 0.6830127018922180770, -0.6830127018922204085, -0.2588190451025213501 ) ) ;
#59492=DIRECTION ( 'NONE',  ( 0.7071067811865486830, -0.7071067811865464625, -0.000000000000000000 ) ) ;
#59493=DIRECTION ( 'NONE',  ( 0.7071067811865487940, -0.7071067811865463515, 0.000000000000000000 ) ) ;
#59495=VECTOR ( 'NONE', #120760, 999.9999999999998863 ) ;
#59496=FACE_BOUND ( 'NONE', #74357, .T. ) ;
#59497=ORIENTED_EDGE ( 'NONE', *, *, #30848, .F. ) ;
#59498=CARTESIAN_POINT ( 'NONE',  ( 31.49999999999979039, 4.087461875839202285, 4.000000000000000000 ) ) ;
#59499=DIRECTION ( 'NONE',  ( 1.000000000000000000, 0.000000000000000000, 0.000000000000000000 ) ) ;
#59500=CARTESIAN_POINT ( 'NONE',  ( -12.48921356237309155, -27.52281430457064104, 5.000000000000000000 ) ) ;
#59501=ORIENTED_EDGE ( 'NONE', *, *, #112706, .F. ) ;
#59503=ORIENTED_EDGE ( 'NONE', *, *, #17190, .F. ) ;
#59505=AXIS2_PLACEMENT_3D ( 'NONE', #21479, #109903, #52661 ) ;
#59506=ORIENTED_EDGE ( 'NONE', *, *, #114859, .F. ) ;
#59507=VECTOR ( 'NONE', #105956, 1000.000000000000000 ) ;
#59509=ORIENTED_EDGE ( 'NONE', *, *, #96244, .F. ) ;
#59511=CARTESIAN_POINT ( 'NONE',  ( -26.20710678118636139, -11.24070752338416845, 5.000000000000000000 ) ) ;
#59512=LINE ( 'NONE', #37755, #12645 ) ;
#59514=VERTEX_POINT ( 'NONE', #69602 ) ;
#59518=DIRECTION ( 'NONE',  ( 0.3543493200069162685, -0.000000000000000000, -0.9351131265310288487 ) ) ;
#59519=CARTESIAN_POINT ( 'NONE',  ( -16.49999999999988631, 21.43112307739196609, 4.000000000000000000 ) ) ;
#59520=LINE ( 'NONE', #104409, #41701 ) ;
#59521=CARTESIAN_POINT ( 'NONE',  ( -34.49999999999976552, 18.05432934483075513, 4.994342998332167660 ) ) ;
#59522=CARTESIAN_POINT ( 'NONE',  ( -39.29974487139159578, -27.71228299555233576, 4.000000000000000000 ) ) ;
#59523=ORIENTED_EDGE ( 'NONE', *, *, #58480, .T. ) ;
#59524=EDGE_CURVE ( 'NONE', #44351, #54134, #113055, .T. ) ;
#59525=VERTEX_POINT ( 'NONE', #102922 ) ;
#59526=ORIENTED_EDGE ( 'NONE', *, *, #83780, .F. ) ;
#59528=DIRECTION ( 'NONE',  ( 0.7071067811865487940, 0.7071067811865463515, -0.000000000000000000 ) ) ;
#59529=EDGE_LOOP ( 'NONE', ( #56387, #139547, #74839, #9839 ) ) ;
#59530=ADVANCED_FACE ( 'NONE', ( #79060 ), #114481, .F. ) ;
#59531=EDGE_LOOP ( 'NONE', ( #30549, #20785, #111541, #37962 ) ) ;
#59532=DIRECTION ( 'NONE',  ( -0.7071067811865486830, 0.7071067811865464625, 0.000000000000000000 ) ) ;
#59534=EDGE_CURVE ( 'NONE', #23978, #102891, #101474, .T. ) ;
#59535=DIRECTION ( 'NONE',  ( 0.7071067811865487940, 0.7071067811865463515, 0.000000000000000000 ) ) ;
#59536=EDGE_LOOP ( 'NONE', ( #112252, #90942, #103443, #27063 ) ) ;
#59537=VECTOR ( 'NONE', #2053, 999.9999999999998863 ) ;
#59538=DIRECTION ( 'NONE',  ( -0.6830127018922180770, -0.6830127018922204085, -0.2588190451025213501 ) ) ;
#59539=ORIENTED_EDGE ( 'NONE', *, *, #55361, .T. ) ;
#59541=ADVANCED_FACE ( 'NONE', ( #23936 ), #100772, .F. ) ;
#59542=EDGE_CURVE ( 'NONE', #19458, #86645, #89879, .T. ) ;
#59543=VECTOR ( 'NONE', #116165, 1000.000000000000000 ) ;
#59546=DIRECTION ( 'NONE',  ( 0.000000000000000000, 0.000000000000000000, -1.000000000000000000 ) ) ;
#59547=EDGE_CURVE ( 'NONE', #98924, #64888, #47169, .T. ) ;
#59548=CARTESIAN_POINT ( 'NONE',  ( 27.18398860626900060, 28.73617430169806042, 5.000000000000000000 ) ) ;
#59549=CARTESIAN_POINT ( 'NONE',  ( 6.183988606268994381, 28.73617430169791476, 5.000000000000000000 ) ) ;
#59550=ORIENTED_EDGE ( 'NONE', *, *, #35190, .T. ) ;
#59551=EDGE_LOOP ( 'NONE', ( #13455, #1739, #55656, #140820 ) ) ;
#59552=EDGE_LOOP ( 'NONE', ( #95800, #11119, #90513, #11309 ) ) ;
#59553=CARTESIAN_POINT ( 'NONE',  ( -74.99451991528749772, 28.92564299267990435, 4.000000000000000000 ) ) ;
#59554=CARTESIAN_POINT ( 'NONE',  ( 0.000000000000000000, 0.000000000000000000, 5.000000000000000000 ) ) ;
#59556=DIRECTION ( 'NONE',  ( -0.6830127018922180770, -0.6830127018922204085, -0.2588190451025213501 ) ) ;
#59559=LINE ( 'NONE', #126901, #52903 ) ;
#59560=EDGE_CURVE ( 'NONE', #125176, #35489, #102219, .T. ) ;
#59561=CARTESIAN_POINT ( 'NONE',  ( 26.51078643762690845, -27.52281430457036748, 5.000000000000000000 ) ) ;
#59562=CARTESIAN_POINT ( 'NONE',  ( 48.48921356237309510, -27.52281430457089328, 5.000000000000000000 ) ) ;
#59563=VECTOR ( 'NONE', #13020, 1000.000000000000000 ) ;
#59564=ORIENTED_EDGE ( 'NONE', *, *, #97132, .F. ) ;
#59565=DIRECTION ( 'NONE',  ( 1.000000000000000000, 0.000000000000000000, 0.000000000000000000 ) ) ;
#59566=CARTESIAN_POINT ( 'NONE',  ( -23.99999999999982592, -6.033600742197678279, 5.000000000000000000 ) ) ;
#59567=EDGE_LOOP ( 'NONE', ( #2834, #136094, #131770, #84313 ) ) ;
#59568=VECTOR ( 'NONE', #115768, 999.9999999999998863 ) ;
#59569=DIRECTION ( 'NONE',  ( -0.7071067811865486830, -0.7071067811865464625, 0.000000000000000000 ) ) ;
#59570=ORIENTED_EDGE ( 'NONE', *, *, #66299, .F. ) ;
#59571=ORIENTED_EDGE ( 'NONE', *, *, #54876, .F. ) ;
#59572=CARTESIAN_POINT ( 'NONE',  ( 3.299744871391591339, -27.71228299555208352, 4.000000000000000000 ) ) ;
#59573=PLANE ( 'NONE',  #32170 ) ;
#59574=ADVANCED_FACE ( 'NONE', ( #73160 ), #126105, .F. ) ;
#59575=ORIENTED_EDGE ( 'NONE', *, *, #10159, .T. ) ;
#59576=FACE_OUTER_BOUND ( 'NONE', #58050, .T. ) ;
#59577=DIRECTION ( 'NONE',  ( -0.6830127018922181881, 0.6830127018922202975, -0.2588190451025214056 ) ) ;
#59578=VECTOR ( 'NONE', #42910, 1000.000000000000000 ) ;
#59579=EDGE_LOOP ( 'NONE', ( #126645, #140624, #136789, #27889 ) ) ;
#59580=CARTESIAN_POINT ( 'NONE',  ( -26.99999999999980105, 5.587461875839189851, 4.000000000000000000 ) ) ;
#59581=LINE ( 'NONE', #103742, #7192 ) ;
#59582=DIRECTION ( 'NONE',  ( 0.3543493200069162685, -0.000000000000000000, -0.9351131265310288487 ) ) ;
#59583=DIRECTION ( 'NONE',  ( 0.6830127018922181881, 0.6830127018922202975, -0.2588190451025214056 ) ) ;
#59584=EDGE_CURVE ( 'NONE', #113044, #94978, #62276, .T. ) ;
#59585=DIRECTION ( 'NONE',  ( 0.7071067811865486830, -0.7071067811865464625, -0.000000000000000000 ) ) ;
#59588=PLANE ( 'NONE',  #70902 ) ;
#59589=ORIENTED_EDGE ( 'NONE', *, *, #30885, .F. ) ;
#59590=ORIENTED_EDGE ( 'NONE', *, *, #25696, .F. ) ;
#59591=ORIENTED_EDGE ( 'NONE', *, *, #49428, .F. ) ;
#59592=EDGE_CURVE ( 'NONE', #129767, #119756, #103598, .T. ) ;
#59594=ORIENTED_EDGE ( 'NONE', *, *, #31839, .T. ) ;
#59595=ORIENTED_EDGE ( 'NONE', *, *, #72735, .T. ) ;
#59596=ADVANCED_FACE ( 'NONE', ( #139121 ), #83306, .F. ) ;
#59599=DIRECTION ( 'NONE',  ( -0.000000000000000000, 0.3543493200069153248, 0.9351131265310292928 ) ) ;
#59600=EDGE_LOOP ( 'NONE', ( #26425, #54611, #6504, #101222 ) ) ;
#59601=EDGE_CURVE ( 'NONE', #1535, #105294, #106430, .T. ) ;
#59602=CARTESIAN_POINT ( 'NONE',  ( 16.49999999999988631, 15.43112307739202471, 4.000000000000000000 ) ) ;
#59603=EDGE_CURVE ( 'NONE', #111091, #131639, #93465, .T. ) ;
#59604=DIRECTION ( 'NONE',  ( 0.6830127018922181881, 0.6830127018922202975, -0.2588190451025214056 ) ) ;
#59605=VECTOR ( 'NONE', #49140, 1000.000000000000227 ) ;
#59606=DIRECTION ( 'NONE',  ( -0.7071067811865487940, 0.7071067811865463515, 0.000000000000000000 ) ) ;
#59609=CARTESIAN_POINT ( 'NONE',  ( 25.49999999999983302, -8.947814304570739452, 5.000000000000000000 ) ) ;
#59610=DIRECTION ( 'NONE',  ( 0.7071067811865487940, -0.7071067811865463515, 0.000000000000000000 ) ) ;
#59611=CARTESIAN_POINT ( 'NONE',  ( -53.99451991528749062, 28.92564299267975869, 4.000000000000000000 ) ) ;
#59612=FACE_OUTER_BOUND ( 'NONE', #135370, .T. ) ;
#59613=CARTESIAN_POINT ( 'NONE',  ( 39.29974487139159578, -27.71228299555233576, 4.000000000000000000 ) ) ;
#59614=EDGE_CURVE ( 'NONE', #142939, #28531, #84049, .T. ) ;
#59615=VECTOR ( 'NONE', #3267, 1000.000000000000227 ) ;
#59616=FACE_OUTER_BOUND ( 'NONE', #96884, .T. ) ;
#59618=VECTOR ( 'NONE', #54670, 1000.000000000000000 ) ;
#59620=DIRECTION ( 'NONE',  ( -0.6830127018922180770, -0.6830127018922204085, -0.2588190451025213501 ) ) ;
#59621=VECTOR ( 'NONE', #140713, 999.9999999999998863 ) ;
#59623=ORIENTED_EDGE ( 'NONE', *, *, #102518, .F. ) ;
#59626=VERTEX_POINT ( 'NONE', #37678 ) ;
#59628=EDGE_CURVE ( 'NONE', #100056, #17934, #50666, .T. ) ;
#59629=PLANE ( 'NONE',  #85666 ) ;
#59630=DIRECTION ( 'NONE',  ( 0.000000000000000000, 0.000000000000000000, -1.000000000000000000 ) ) ;
#59631=VECTOR ( 'NONE', #42162, 999.9999999999998863 ) ;
#59633=FACE_OUTER_BOUND ( 'NONE', #118, .T. ) ;
#59634=CARTESIAN_POINT ( 'NONE',  ( 13.49999999999990585, -13.53360074219760101, 5.000000000000000000 ) ) ;
#59637=EDGE_LOOP ( 'NONE', ( #10694, #28330, #119691, #39139 ) ) ;
#59638=CARTESIAN_POINT ( 'NONE',  ( 63.48921356237309510, -27.52281430457099631, 5.000000000000000000 ) ) ;
#59640=FACE_OUTER_BOUND ( 'NONE', #4751, .T. ) ;
#59641=PLANE ( 'NONE',  #87014 ) ;
#59642=DIRECTION ( 'NONE',  ( 0.7071067811865487940, 0.7071067811865463515, 0.000000000000000000 ) ) ;
#59645=ORIENTED_EDGE ( 'NONE', *, *, #75911, .T. ) ;
#59647=PLANE ( 'NONE',  #60141 ) ;
#59648=CARTESIAN_POINT ( 'NONE',  ( 1.171830600776468057, 21.75929247661549581, 4.000000000000000000 ) ) ;
#59649=VECTOR ( 'NONE', #3296, 1000.000000000000227 ) ;
#59650=LINE ( 'NONE', #102439, #92649 ) ;
#59651=EDGE_CURVE ( 'NONE', #131487, #28495, #82587, .T. ) ;
#59653=EDGE_LOOP ( 'NONE', ( #131702, #94892, #41228, #7907 ) ) ;
#59654=LINE ( 'NONE', #92232, #113658 ) ;
#59655=CARTESIAN_POINT ( 'NONE',  ( -45.29974487139158867, -27.71228299555237840, 4.000000000000000000 ) ) ;
#59656=VERTEX_POINT ( 'NONE', #4977 ) ;
#59657=ORIENTED_EDGE ( 'NONE', *, *, #135980, .T. ) ;
#59659=CARTESIAN_POINT ( 'NONE',  ( 3.299744871391591339, -27.71228299555208352, 4.000000000000000000 ) ) ;
#59660=ORIENTED_EDGE ( 'NONE', *, *, #56801, .T. ) ;
#59661=EDGE_CURVE ( 'NONE', #134832, #36043, #15846, .T. ) ;
#59662=( BOUNDED_CURVE ( )  B_SPLINE_CURVE ( 3, ( #11470, #610, #67334, #33307 ),
 .UNSPECIFIED., .F., .T. ) 
 B_SPLINE_CURVE_WITH_KNOTS ( ( 4, 4 ),
 ( 4.350170835173026163, 4.500739107949258688 ),
 .UNSPECIFIED. ) 
 CURVE ( )  GEOMETRIC_REPRESENTATION_ITEM ( )  RATIONAL_B_SPLINE_CURVE ( ( 1.000000000000000000, 0.9981116584018945304, 0.9981116584018945304, 1.000000000000000000 ) ) 
 REPRESENTATION_ITEM ( '' )  );
#59663=ADVANCED_FACE ( 'NONE', ( #49278 ), #138393, .F. ) ;
#59665=EDGE_LOOP ( 'NONE', ( #88413, #33998, #88805, #130629 ) ) ;
#59668=FACE_BOUND ( 'NONE', #45772, .T. ) ;
#59669=EDGE_CURVE ( 'NONE', #132816, #55582, #16597, .T. ) ;
#59671=LINE ( 'NONE', #37916, #83799 ) ;
#59672=CARTESIAN_POINT ( 'NONE',  ( 25.49999999999982236, -14.56887692260766087, 4.000000000000000000 ) ) ;
#59673=LINE ( 'NONE', #50214, #112958 ) ;
#59674=ORIENTED_EDGE ( 'NONE', *, *, #70586, .T. ) ;
#59675=DIRECTION ( 'NONE',  ( 0.7071067811865487940, 0.7071067811865463515, 0.000000000000000000 ) ) ;
#59677=VERTEX_POINT ( 'NONE', #61580 ) ;
#59680=AXIS2_PLACEMENT_3D ( 'NONE', #13446, #57721, #67910 ) ;
#59681=LINE ( 'NONE', #37190, #6970 ) ;
#59682=CARTESIAN_POINT ( 'NONE',  ( -22.49999999999983658, 19.46639925780206326, 5.000000000000000000 ) ) ;
#59683=ORIENTED_EDGE ( 'NONE', *, *, #29537, .T. ) ;
#59685=VECTOR ( 'NONE', #83683, 1000.000000000000000 ) ;
#59686=EDGE_CURVE ( 'NONE', #38538, #135052, #49974, .T. ) ;
#59687=LINE ( 'NONE', #60408, #128870 ) ;
#59689=CARTESIAN_POINT ( 'NONE',  ( -26.29298673570676925, -21.74070752338405299, 4.999753212805220670 ) ) ;
#59690=CARTESIAN_POINT ( 'NONE',  ( 32.99999999999977263, 1.761378380278715738, -6.096875308897179657 ) ) ;
#59691=DIRECTION ( 'NONE',  ( -0.6830127018922180770, -0.6830127018922204085, -0.2588190451025213501 ) ) ;
#59692=ORIENTED_EDGE ( 'NONE', *, *, #10892, .F. ) ;
#59693=ORIENTED_EDGE ( 'NONE', *, *, #19898, .F. ) ;
#59694=LINE ( 'NONE', #39369, #82151 ) ;
#59695=VECTOR ( 'NONE', #109798, 1000.000000000000000 ) ;
#59697=ORIENTED_EDGE ( 'NONE', *, *, #40117, .T. ) ;
#59698=ORIENTED_EDGE ( 'NONE', *, *, #131636, .F. ) ;
#59699=VECTOR ( 'NONE', #76608, 1000.000000000000000 ) ;
#59700=VERTEX_POINT ( 'NONE', #137476 ) ;
#59701=LINE ( 'NONE', #16133, #4894 ) ;
#59702=EDGE_CURVE ( 'NONE', #91750, #77043, #6901, .T. ) ;
#59703=DIRECTION ( 'NONE',  ( 0.7071067811865487940, 0.7071067811865463515, 0.000000000000000000 ) ) ;
#59704=ORIENTED_EDGE ( 'NONE', *, *, #111232, .F. ) ;
#59705=CARTESIAN_POINT ( 'NONE',  ( -3.792893218813424117, -17.24070752338410628, 5.000000000000000000 ) ) ;
#59706=AXIS2_PLACEMENT_3D ( 'NONE', #60206, #103655, #4298 ) ;
#59707=VECTOR ( 'NONE', #21847, 1000.000000000000000 ) ;
#59708=LINE ( 'NONE', #50960, #141950 ) ;
#59710=EDGE_CURVE ( 'NONE', #40577, #138063, #91804, .T. ) ;
#59712=DIRECTION ( 'NONE',  ( 0.7071067811865487940, 0.7071067811865463515, -0.000000000000000000 ) ) ;
#59714=ORIENTED_EDGE ( 'NONE', *, *, #77343, .T. ) ;
#59715=CARTESIAN_POINT ( 'NONE',  ( -6.656710001662093923, 3.759292476615674783, 13.27625715073264168 ) ) ;
#59716=ADVANCED_FACE ( 'NONE', ( #6190 ), #128042, .T. ) ;
#59718=CARTESIAN_POINT ( 'NONE',  ( -32.99999999999976552, -11.35517001088074629, -1.126524801160187161 ) ) ;
#59719=PLANE ( 'NONE',  #58805 ) ;
#59723=EDGE_CURVE ( 'NONE', #32684, #7267, #49046, .T. ) ;
#59724=DIRECTION ( 'NONE',  ( -0.000000000000000000, 0.000000000000000000, 1.000000000000000000 ) ) ;
#59725=PLANE ( 'NONE',  #141942 ) ;
#59729=EDGE_CURVE ( 'NONE', #31893, #78216, #136734, .T. ) ;
#59730=DIRECTION ( 'NONE',  ( -0.3543493200069162685, -0.000000000000000000, -0.9351131265310288487 ) ) ;
#59732=DIRECTION ( 'NONE',  ( -0.7071067811865486830, -0.7071067811865464625, 0.000000000000000000 ) ) ;
#59733=VERTEX_POINT ( 'NONE', #117122 ) ;
#59734=CARTESIAN_POINT ( 'NONE',  ( 36.18398860626899705, 28.73617430169812437, 5.000000000000000000 ) ) ;
#59735=DIRECTION ( 'NONE',  ( 0.3543493200069163240, -0.000000000000000000, -0.9351131265310288487 ) ) ;
#59737=EDGE_CURVE ( 'NONE', #25222, #51133, #138185, .T. ) ;
#59743=CARTESIAN_POINT ( 'NONE',  ( -42.48921356237308800, -27.52281430457085065, 5.000000000000000000 ) ) ;
#59745=ADVANCED_FACE ( 'NONE', ( #14951 ), #104828, .F. ) ;
#59747=LINE ( 'NONE', #103907, #99101 ) ;
#59748=CARTESIAN_POINT ( 'NONE',  ( 25.82816939922335209, -20.24070752338407431, 4.000000000000000000 ) ) ;
#59750=DIRECTION ( 'NONE',  ( -0.7071067811865486830, 0.7071067811865464625, 0.000000000000000000 ) ) ;
#59752=DIRECTION ( 'NONE',  ( -0.7071067811865486830, 0.7071067811865464625, 0.000000000000000000 ) ) ;
#59753=CARTESIAN_POINT ( 'NONE',  ( 0.1839886062690032631, 28.73617430169787568, 5.000000000000000000 ) ) ;
#59756=( BOUNDED_CURVE ( )  B_SPLINE_CURVE ( 3, ( #118946, #87757, #87045, #55868 ),
 .UNSPECIFIED., .F., .F. ) 
 B_SPLINE_CURVE_WITH_KNOTS ( ( 4, 4 ),
 ( 0.6873533248919960759, 0.6988790395524697718 ),
 .UNSPECIFIED. ) 
 CURVE ( )  GEOMETRIC_REPRESENTATION_ITEM ( )  RATIONAL_B_SPLINE_CURVE ( ( 1.000000000000000000, 0.9999889298557675943, 0.9999889298557675943, 1.000000000000000000 ) ) 
 REPRESENTATION_ITEM ( '' )  );
#59757=DIRECTION ( 'NONE',  ( 0.6830127018922180770, -0.6830127018922204085, -0.2588190451025213501 ) ) ;
#59758=ORIENTED_EDGE ( 'NONE', *, *, #44240, .T. ) ;
#59759=CARTESIAN_POINT ( 'NONE',  ( -34.75611968250421313, 5.812934254707314174, 4.955485411084895375 ) ) ;
#59760=VERTEX_POINT ( 'NONE', #125153 ) ;
#59761=LINE ( 'NONE', #59074, #122407 ) ;
#59762=EDGE_CURVE ( 'NONE', #77708, #139000, #62070, .T. ) ;
#59765=DIRECTION ( 'NONE',  ( -0.000000000000000000, 0.000000000000000000, 1.000000000000000000 ) ) ;
#59766=CARTESIAN_POINT ( 'NONE',  ( -34.92500000000001137, 12.85612307739231497, 4.000000000000000000 ) ) ;
#59767=CARTESIAN_POINT ( 'NONE',  ( -25.49999999999982236, -12.08601207473290451, -10.46905243149087994 ) ) ;
#59769=CARTESIAN_POINT ( 'NONE',  ( -36.48921356237310221, -27.52281430457080802, 5.000000000000000000 ) ) ;
#59770=ORIENTED_EDGE ( 'NONE', *, *, #56358, .F. ) ;
#59772=DIRECTION ( 'NONE',  ( -0.7071067811865486830, 0.7071067811865464625, 0.000000000000000000 ) ) ;
#59773=DIRECTION ( 'NONE',  ( 0.000000000000000000, 1.000000000000000000, 0.000000000000000000 ) ) ;
#59775=LINE ( 'NONE', #123621, #38772 ) ;
#59779=ORIENTED_EDGE ( 'NONE', *, *, #38097, .T. ) ;
#59780=VECTOR ( 'NONE', #11666, 1000.000000000000227 ) ;
#59782=FACE_OUTER_BOUND ( 'NONE', #36733, .T. ) ;
#59784=DIRECTION ( 'NONE',  ( 1.000000000000000000, 0.000000000000000000, 0.000000000000000000 ) ) ;
#59785=CARTESIAN_POINT ( 'NONE',  ( 12.00548008471251293, 28.92564299267929684, 4.000000000000000000 ) ) ;
#59786=ORIENTED_EDGE ( 'NONE', *, *, #69458, .T. ) ;
#59787=DIRECTION ( 'NONE',  ( 0.3543493200069163240, 0.000000000000000000, 0.9351131265310288487 ) ) ;
#59788=EDGE_CURVE ( 'NONE', #140843, #43910, #30867, .T. ) ;
#59789=LINE ( 'NONE', #17666, #120779 ) ;
#59791=FACE_OUTER_BOUND ( 'NONE', #2887, .T. ) ;
#59792=ORIENTED_EDGE ( 'NONE', *, *, #14861, .T. ) ;
#59795=AXIS2_PLACEMENT_3D ( 'NONE', #51337, #40472, #6335 ) ;
#59796=DIRECTION ( 'NONE',  ( 0.7071067811865487940, 0.7071067811865463515, 0.000000000000000000 ) ) ;
#59797=CARTESIAN_POINT ( 'NONE',  ( -28.49999999999980460, -14.70932175296479549, -11.46312253303830353 ) ) ;
#59798=AXIS2_PLACEMENT_3D ( 'NONE', #140932, #41626, #87288 ) ;
#59799=DIRECTION ( 'NONE',  ( 0.7071067811865487940, -0.7071067811865463515, -0.000000000000000000 ) ) ;
#59800=EDGE_CURVE ( 'NONE', #14639, #83008, #18505, .T. ) ;
#59801=DIRECTION ( 'NONE',  ( -0.6830127018922180770, -0.6830127018922204085, -0.2588190451025213501 ) ) ;
#59803=EDGE_LOOP ( 'NONE', ( #33088, #100254, #34384, #90280 ) ) ;
#59804=DIRECTION ( 'NONE',  ( -0.7071067811865486830, 0.7071067811865464625, 0.000000000000000000 ) ) ;
#59806=VECTOR ( 'NONE', #18620, 1000.000000000000227 ) ;
#59807=CARTESIAN_POINT ( 'NONE',  ( 1.499999999999994449, 10.94296225409026668, -9.576120664313254593 ) ) ;
#59808=VECTOR ( 'NONE', #48604, 1000.000000000000000 ) ;
#59809=ORIENTED_EDGE ( 'NONE', *, *, #111933, .F. ) ;
#59810=ORIENTED_EDGE ( 'NONE', *, *, #110697, .T. ) ;
#59812=DIRECTION ( 'NONE',  ( 0.3543493200069162685, -0.000000000000000000, -0.9351131265310288487 ) ) ;
#59814=LINE ( 'NONE', #17010, #136063 ) ;
#59815=CARTESIAN_POINT ( 'NONE',  ( -34.92500000000001137, 14.71849043720408190, 4.759050581649336920 ) ) ;
#59816=VERTEX_POINT ( 'NONE', #74366 ) ;
#59817=EDGE_LOOP ( 'NONE', ( #134197, #6642, #19596, #138617 ) ) ;
#59818=CARTESIAN_POINT ( 'NONE',  ( 0.000000000000000000, 0.000000000000000000, 5.000000000000000000 ) ) ;
#59819=CARTESIAN_POINT ( 'NONE',  ( -57.18398860626899705, 28.73617430169827358, 5.000000000000000000 ) ) ;
#59820=EDGE_CURVE ( 'NONE', #55488, #96120, #96082, .T. ) ;
#59821=VERTEX_POINT ( 'NONE', #31568 ) ;
#59822=EDGE_CURVE ( 'NONE', #50417, #41659, #19953, .T. ) ;
#59823=CARTESIAN_POINT ( 'NONE',  ( 29.99451991528749417, 28.92564299267958816, 4.000000000000000000 ) ) ;
#59824=VERTEX_POINT ( 'NONE', #73640 ) ;
#59825=PLANE ( 'NONE',  #91962 ) ;
#59828=VECTOR ( 'NONE', #5316, 999.9999999999998863 ) ;
#59829=AXIS2_PLACEMENT_3D ( 'NONE', #139220, #109417, #40610 ) ;
#59830=FACE_BOUND ( 'NONE', #16424, .T. ) ;
#59831=ADVANCED_FACE ( 'NONE', ( #41007 ), #62780, .T. ) ;
#59832=FACE_OUTER_BOUND ( 'NONE', #64495, .T. ) ;
#59833=PLANE ( 'NONE',  #23532 ) ;
#59834=DIRECTION ( 'NONE',  ( -0.3543493200069162685, -0.000000000000000000, -0.9351131265310288487 ) ) ;
#59835=DIRECTION ( 'NONE',  ( 0.7071067811865487940, 0.7071067811865463515, 0.000000000000000000 ) ) ;
#59836=CARTESIAN_POINT ( 'NONE',  ( -9.707106781186469746, 20.25929247661551713, 5.000000000000000000 ) ) ;
#59838=ORIENTED_EDGE ( 'NONE', *, *, #36333, .T. ) ;
#59839=ORIENTED_EDGE ( 'NONE', *, *, #5532, .F. ) ;
#59841=ORIENTED_EDGE ( 'NONE', *, *, #81638, .F. ) ;
#59842=DIRECTION ( 'NONE',  ( 0.000000000000000000, 1.000000000000000000, 0.000000000000000000 ) ) ;
#59843=DIRECTION ( 'NONE',  ( -0.6830127018922181881, 0.6830127018922202975, -0.2588190451025214056 ) ) ;
#59844=AXIS2_PLACEMENT_3D ( 'NONE', #117405, #31162, #16685 ) ;
#59845=VECTOR ( 'NONE', #16359, 999.9999999999998863 ) ;
#59847=ORIENTED_EDGE ( 'NONE', *, *, #78528, .T. ) ;
#59848=DIRECTION ( 'NONE',  ( -0.3543493200069162685, -0.000000000000000000, -0.9351131265310288487 ) ) ;
#59849=CARTESIAN_POINT ( 'NONE',  ( 8.207106781186489286, 12.75929247661558996, 5.000000000000000000 ) ) ;
#59850=LINE ( 'NONE', #27194, #75903 ) ;
#59852=LINE ( 'NONE', #116361, #72904 ) ;
#59853=FACE_OUTER_BOUND ( 'NONE', #47816, .T. ) ;
#59854=CARTESIAN_POINT ( 'NONE',  ( 17.99999999999988276, -13.44781430457068794, 5.000000000000000000 ) ) ;
#59856=CARTESIAN_POINT ( 'NONE',  ( -63.18398860626900415, 28.73617430169831621, 5.000000000000000000 ) ) ;
#59857=PLANE ( 'NONE',  #102087 ) ;
#59858=VERTEX_POINT ( 'NONE', #51180 ) ;
#59859=ORIENTED_EDGE ( 'NONE', *, *, #91218, .F. ) ;
#59860=ORIENTED_EDGE ( 'NONE', *, *, #92806, .T. ) ;
#59862=ORIENTED_EDGE ( 'NONE', *, *, #110427, .T. ) ;
#59863=EDGE_CURVE ( 'NONE', #98856, #9144, #75791, .T. ) ;
#59866=ORIENTED_EDGE ( 'NONE', *, *, #73135, .T. ) ;
#59867=EDGE_CURVE ( 'NONE', #101632, #15581, #139645, .T. ) ;
#59868=LINE ( 'NONE', #59187, #1628 ) ;
#59869=ADVANCED_FACE ( 'NONE', ( #52587, #20665 ), #40325, .F. ) ;
#59870=EDGE_LOOP ( 'NONE', ( #104385, #92405, #123854, #99229 ) ) ;
#59871=CARTESIAN_POINT ( 'NONE',  ( -2.200031220168353840, 8.259292476615634371, 16.85664084051841627 ) ) ;
#59872=CARTESIAN_POINT ( 'NONE',  ( -1.499999999999987566, -4.533600742197694267, 5.000000000000000000 ) ) ;
#59874=ORIENTED_EDGE ( 'NONE', *, *, #137724, .F. ) ;
#59875=ORIENTED_EDGE ( 'NONE', *, *, #27567, .F. ) ;
#59876=EDGE_CURVE ( 'NONE', #28133, #34213, #86670, .T. ) ;
#59878=DIRECTION ( 'NONE',  ( -0.3543493200069162685, -0.000000000000000000, -0.9351131265310288487 ) ) ;
#59879=ORIENTED_EDGE ( 'NONE', *, *, #17301, .F. ) ;
#59880=LINE ( 'NONE', #38136, #64334 ) ;
#59881=VERTEX_POINT ( 'NONE', #32283 ) ;
#59882=VECTOR ( 'NONE', #93596, 1000.000000000000000 ) ;
#59884=VERTEX_POINT ( 'NONE', #117816 ) ;
#59886=CARTESIAN_POINT ( 'NONE',  ( 30.48921356237309510, -27.52281430457076894, 5.000000000000000000 ) ) ;
#59888=AXIS2_PLACEMENT_3D ( 'NONE', #23689, #90369, #36697 ) ;
#59889=VECTOR ( 'NONE', #41438, 1000.000000000000000 ) ;
#59890=DIRECTION ( 'NONE',  ( 0.7071067811865486830, 0.7071067811865464625, 0.000000000000000000 ) ) ;
#59891=AXIS2_PLACEMENT_3D ( 'NONE', #125804, #124361, #25030 ) ;
#59892=EDGE_CURVE ( 'NONE', #98193, #105689, #30118, .T. ) ;
#59893=LINE ( 'NONE', #58512, #88793 ) ;
#59894=CARTESIAN_POINT ( 'NONE',  ( -29.20710678118633652, 18.75929247661552779, 5.000000000000000000 ) ) ;
#59895=EDGE_CURVE ( 'NONE', #62344, #8091, #9793, .T. ) ;
#59896=AXIS2_PLACEMENT_3D ( 'NONE', #56379, #23699, #10653 ) ;
#59897=LINE ( 'NONE', #67954, #136824 ) ;
#59898=ORIENTED_EDGE ( 'NONE', *, *, #138396, .F. ) ;
#59899=AXIS2_PLACEMENT_3D ( 'NONE', #82003, #5790, #128337 ) ;
#59900=VECTOR ( 'NONE', #116245, 1000.000000000000227 ) ;
#59902=EDGE_CURVE ( 'NONE', #101225, #19552, #141017, .T. ) ;
#59905=LINE ( 'NONE', #49759, #32145 ) ;
#59906=( BOUNDED_CURVE ( )  B_SPLINE_CURVE ( 3, ( #136159, #80385, #78961, #126018 ),
 .UNSPECIFIED., .F., .T. ) 
 B_SPLINE_CURVE_WITH_KNOTS ( ( 4, 4 ),
 ( 4.257860004652494368, 4.307247239014357021 ),
 .UNSPECIFIED. ) 
 CURVE ( )  GEOMETRIC_REPRESENTATION_ITEM ( )  RATIONAL_B_SPLINE_CURVE ( ( 1.000000000000000000, 0.9997967520851089862, 0.9997967520851089862, 1.000000000000000000 ) ) 
 REPRESENTATION_ITEM ( '' )  );
#59907=FACE_OUTER_BOUND ( 'NONE', #71881, .T. ) ;
#59908=ORIENTED_EDGE ( 'NONE', *, *, #4569, .T. ) ;
#59909=ORIENTED_EDGE ( 'NONE', *, *, #108251, .T. ) ;
#59911=CARTESIAN_POINT ( 'NONE',  ( 14.28769006033961375, -21.73547319004781642, 4.999917730833664642 ) ) ;
#59912=CARTESIAN_POINT ( 'NONE',  ( 34.92499999999998295, 1.821246448331339307, 12.73174495308783705 ) ) ;
#59914=PLANE ( 'NONE',  #84702 ) ;
#59917=DIRECTION ( 'NONE',  ( -0.000000000000000000, -0.3543493200069152693, 0.9351131265310292928 ) ) ;
#59918=FACE_OUTER_BOUND ( 'NONE', #95906, .T. ) ;
#59920=DIRECTION ( 'NONE',  ( -0.7071067811865487940, 0.7071067811865463515, -0.000000000000000000 ) ) ;
#59921=PLANE ( 'NONE',  #131740 ) ;
#59922=DIRECTION ( 'NONE',  ( 0.7071067811865487940, -0.7071067811865463515, 0.000000000000000000 ) ) ;
#59923=DIRECTION ( 'NONE',  ( -0.7071067811865487940, 0.7071067811865463515, 0.000000000000000000 ) ) ;
#59924=CARTESIAN_POINT ( 'NONE',  ( 48.29974487139158867, -27.71228299555239971, 4.000000000000000000 ) ) ;
#59925=EDGE_CURVE ( 'NONE', #128596, #5408, #130173, .T. ) ;
#59926=ORIENTED_EDGE ( 'NONE', *, *, #131646, .T. ) ;
#59927=VECTOR ( 'NONE', #129088, 1000.000000000000000 ) ;
#59928=CARTESIAN_POINT ( 'NONE',  ( -34.42500000000001137, 22.22500000000000142, 4.165035510187088619 ) ) ;
#59929=EDGE_LOOP ( 'NONE', ( #520, #126514, #102062, #65351 ) ) ;
#59930=VECTOR ( 'NONE', #121274, 1000.000000000000000 ) ;
#59931=VECTOR ( 'NONE', #108367, 1000.000000000000000 ) ;
#59932=AXIS2_PLACEMENT_3D ( 'NONE', #52058, #140475, #130341 ) ;
#59933=CARTESIAN_POINT ( 'NONE',  ( 0.2782545156857219038, 8.259292476615637923, 11.78515199841150363 ) ) ;
#59935=EDGE_LOOP ( 'NONE', ( #27971, #41840, #78943, #76677 ) ) ;
#59936=CARTESIAN_POINT ( 'NONE',  ( 26.47599861414532185, 22.03583458319438293, 4.979811245910084949 ) ) ;
#59939=DIRECTION ( 'NONE',  ( 0.6830127018922181881, 0.6830127018922202975, -0.2588190451025214056 ) ) ;
#59940=VERTEX_POINT ( 'NONE', #51902 ) ;
#59941=DIRECTION ( 'NONE',  ( -0.000000000000000000, -1.000000000000000000, -0.000000000000000000 ) ) ;
#59942=VERTEX_POINT ( 'NONE', #64197 ) ;
#59943=VECTOR ( 'NONE', #33397, 1000.000000000000000 ) ;
#59945=DIRECTION ( 'NONE',  ( 0.6830127018922181881, 0.6830127018922202975, -0.2588190451025214056 ) ) ;
#59946=ADVANCED_FACE ( 'NONE', ( #108356 ), #9032, .F. ) ;
#59948=LINE ( 'NONE', #102728, #111076 ) ;
#59950=ORIENTED_EDGE ( 'NONE', *, *, #14392, .T. ) ;
#59952=ADVANCED_FACE ( 'NONE', ( #123600 ), #46029, .F. ) ;
#59953=CARTESIAN_POINT ( 'NONE',  ( -66.18398860626901126, 28.73617430169833753, 5.000000000000000000 ) ) ;
#59955=AXIS2_PLACEMENT_3D ( 'NONE', #119240, #8315, #52565 ) ;
#59959=EDGE_CURVE ( 'NONE', #97151, #79079, #34414, .T. ) ;
#59961=DIRECTION ( 'NONE',  ( -0.7071067811865486830, -0.7071067811865464625, 0.000000000000000000 ) ) ;
#59962=CARTESIAN_POINT ( 'NONE',  ( -27.79289321881325847, -5.240707523384227073, 5.000000000000000000 ) ) ;
#59963=CARTESIAN_POINT ( 'NONE',  ( 26.99999999999980815, -9.412538124160658271, 4.000000000000000000 ) ) ;
#59964=ORIENTED_EDGE ( 'NONE', *, *, #11265, .T. ) ;
#59965=LINE ( 'NONE', #128085, #127609 ) ;
#59967=DIRECTION ( 'NONE',  ( -0.6830127018922180770, -0.6830127018922204085, -0.2588190451025213501 ) ) ;
#59968=EDGE_CURVE ( 'NONE', #111985, #94939, #89504, .T. ) ;
#59969=CARTESIAN_POINT ( 'NONE',  ( -24.18398860626899705, 28.73617430169804265, 5.000000000000000000 ) ) ;
#59970=ORIENTED_EDGE ( 'NONE', *, *, #132773, .F. ) ;
#59971=LINE ( 'NONE', #51951, #48640 ) ;
#59972=FACE_OUTER_BOUND ( 'NONE', #65194, .T. ) ;
#59975=ORIENTED_EDGE ( 'NONE', *, *, #38366, .T. ) ;
#59976=EDGE_LOOP ( 'NONE', ( #55835, #51821, #121152, #129110 ) ) ;
#59977=ORIENTED_EDGE ( 'NONE', *, *, #128762, .T. ) ;
#59979=ORIENTED_EDGE ( 'NONE', *, *, #79749, .T. ) ;
#59981=EDGE_CURVE ( 'NONE', #49206, #108133, #90214, .T. ) ;
#59983=CARTESIAN_POINT ( 'NONE',  ( 25.49999999999982592, 15.43112307739203182, 4.000000000000000000 ) ) ;
#59984=CARTESIAN_POINT ( 'NONE',  ( -34.92500000000001137, 22.22500000000000142, 4.000000000000000000 ) ) ;
#59985=ORIENTED_EDGE ( 'NONE', *, *, #102795, .F. ) ;
#59986=FACE_OUTER_BOUND ( 'NONE', #50429, .T. ) ;
#59987=CARTESIAN_POINT ( 'NONE',  ( -26.99451991528749417, 28.92564299267956685, 4.000000000000000000 ) ) ;
#59989=ORIENTED_EDGE ( 'NONE', *, *, #41185, .F. ) ;
#59990=AXIS2_PLACEMENT_3D ( 'NONE', #38501, #82723, #27600 ) ;
#59991=EDGE_CURVE ( 'NONE', #121862, #92108, #133738, .T. ) ;
#59992=DIRECTION ( 'NONE',  ( -0.7071067811865487940, 0.7071067811865463515, 0.000000000000000000 ) ) ;
#59995=FACE_OUTER_BOUND ( 'NONE', #6404, .T. ) ;
#59996=AXIS2_PLACEMENT_3D ( 'NONE', #132445, #55570, #122957 ) ;
#59997=VECTOR ( 'NONE', #132320, 999.9999999999998863 ) ;
#59998=ORIENTED_EDGE ( 'NONE', *, *, #13634, .F. ) ;
#59999=ORIENTED_EDGE ( 'NONE', *, *, #64213, .T. ) ;
#60000=AXIS2_PLACEMENT_3D ( 'NONE', #136302, #124721, #69660 ) ;
#60001=EDGE_CURVE ( 'NONE', #139533, #43222, #69197, .T. ) ;
#60003=EDGE_CURVE ( 'NONE', #25969, #39717, #124277, .T. ) ;
#60004=CARTESIAN_POINT ( 'NONE',  ( 5.999999999999959144, 13.55218569542903140, 5.000000000000000000 ) ) ;
#60005=FACE_OUTER_BOUND ( 'NONE', #86361, .T. ) ;
#60006=DIRECTION ( 'NONE',  ( 0.7071067811865487940, 0.7071067811865463515, 0.000000000000000000 ) ) ;
#60007=VECTOR ( 'NONE', #64013, 1000.000000000000000 ) ;
#60008=CARTESIAN_POINT ( 'NONE',  ( -8.700255128608413102, -27.71228299555199825, 4.000000000000000000 ) ) ;
#60009=DIRECTION ( 'NONE',  ( -0.6830127018922181881, 0.6830127018922202975, -0.2588190451025214056 ) ) ;
#60010=PLANE ( 'NONE',  #92814 ) ;
#60014=ORIENTED_EDGE ( 'NONE', *, *, #94034, .F. ) ;
#60015=VECTOR ( 'NONE', #132911, 1000.000000000000000 ) ;
#60016=EDGE_CURVE ( 'NONE', #22653, #103007, #33026, .T. ) ;
#60017=CARTESIAN_POINT ( 'NONE',  ( -51.29974487139158867, -27.71228299555242103, 4.000000000000000000 ) ) ;
#60018=AXIS2_PLACEMENT_3D ( 'NONE', #69794, #4417, #72665 ) ;
#60019=LINE ( 'NONE', #26659, #135379 ) ;
#60020=EDGE_LOOP ( 'NONE', ( #24655, #143554, #16026, #128775 ) ) ;
#60021=LINE ( 'NONE', #4854, #57525 ) ;
#60022=DIRECTION ( 'NONE',  ( -0.3543493200069162685, -0.000000000000000000, -0.9351131265310288487 ) ) ;
#60023=LINE ( 'NONE', #117212, #45712 ) ;
#60024=CARTESIAN_POINT ( 'NONE',  ( -15.18398860626900237, 28.73617430169797871, 5.000000000000000000 ) ) ;
#60025=AXIS2_PLACEMENT_3D ( 'NONE', #141820, #32335, #75842 ) ;
#60026=CARTESIAN_POINT ( 'NONE',  ( 44.99451991528749772, 28.92564299267969474, 4.000000000000000000 ) ) ;
#60027=ORIENTED_EDGE ( 'NONE', *, *, #83584, .T. ) ;
#60029=CARTESIAN_POINT ( 'NONE',  ( 6.489213562373093325, -27.52281430457059841, 5.000000000000000000 ) ) ;
#60030=LINE ( 'NONE', #125275, #51083 ) ;
#60031=AXIS2_PLACEMENT_3D ( 'NONE', #79765, #68174, #37655 ) ;
#60032=ORIENTED_EDGE ( 'NONE', *, *, #66937, .T. ) ;
#60033=CARTESIAN_POINT ( 'NONE',  ( 34.92499999999998295, -21.72500000000000142, 0.4999999999999995559 ) ) ;
#60034=ORIENTED_EDGE ( 'NONE', *, *, #24807, .F. ) ;
#60035=ORIENTED_EDGE ( 'NONE', *, *, #85773, .T. ) ;
#60036=CARTESIAN_POINT ( 'NONE',  ( -1.499999999999987566, 10.94296225409026668, -9.576120664313261699 ) ) ;
#60037=ORIENTED_EDGE ( 'NONE', *, *, #71256, .F. ) ;
#60038=ORIENTED_EDGE ( 'NONE', *, *, #16365, .T. ) ;
#60039=EDGE_CURVE ( 'NONE', #143112, #81113, #133045, .T. ) ;
#60041=VECTOR ( 'NONE', #78131, 1000.000000000000000 ) ;
#60044=CARTESIAN_POINT ( 'NONE',  ( 15.48921356237309510, -27.52281430457066236, 5.000000000000000000 ) ) ;
#60045=EDGE_CURVE ( 'NONE', #121396, #72622, #135189, .T. ) ;
#60046=CARTESIAN_POINT ( 'NONE',  ( 33.32816939922329169, -3.740707523384255495, 4.000000000000000000 ) ) ;
#60048=DIRECTION ( 'NONE',  ( -0.6830127018922181881, 0.6830127018922202975, -0.2588190451025214056 ) ) ;
#60049=ADVANCED_FACE ( 'NONE', ( #10499 ), #77934, .F. ) ;
#60051=FACE_OUTER_BOUND ( 'NONE', #85976, .T. ) ;
#60052=LINE ( 'NONE', #15081, #106504 ) ;
#60053=VECTOR ( 'NONE', #2263, 1000.000000000000000 ) ;
#60054=CARTESIAN_POINT ( 'NONE',  ( -18.48921356237309510, -27.52281430457068367, 5.000000000000000000 ) ) ;
#60055=EDGE_CURVE ( 'NONE', #12218, #70973, #11187, .T. ) ;
#60057=DIRECTION ( 'NONE',  ( -0.7071067811865487940, 0.7071067811865463515, -0.000000000000000000 ) ) ;
#60058=CARTESIAN_POINT ( 'NONE',  ( 2.306730066903996068, -3.740707523384241728, 12.88036043432867039 ) ) ;
#60059=ORIENTED_EDGE ( 'NONE', *, *, #42293, .F. ) ;
#60060=FACE_OUTER_BOUND ( 'NONE', #5795, .T. ) ;
#60061=EDGE_LOOP ( 'NONE', ( #37404, #70433, #77685, #48836 ) ) ;
#60062=EDGE_LOOP ( 'NONE', ( #26621, #5626, #15810, #89293 ) ) ;
#60064=ORIENTED_EDGE ( 'NONE', *, *, #91449, .T. ) ;
#60065=LINE ( 'NONE', #14403, #102351 ) ;
#60068=CARTESIAN_POINT ( 'NONE',  ( 13.96659967656969314, 6.759292476615649470, 12.28218704918525361 ) ) ;
#60069=ADVANCED_FACE ( 'NONE', ( #77242 ), #12646, .F. ) ;
#60070=CARTESIAN_POINT ( 'NONE',  ( 18.79289321881332597, 15.75929247661555976, 5.000000000000000000 ) ) ;
#60072=DIRECTION ( 'NONE',  ( 0.7071067811865486830, -0.7071067811865464625, -0.000000000000000000 ) ) ;
#60073=ORIENTED_EDGE ( 'NONE', *, *, #6083, .T. ) ;
#60074=CARTESIAN_POINT ( 'NONE',  ( -23.67183060077630330, 20.25929247661551003, 4.000000000000000000 ) ) ;
#60075=ADVANCED_FACE ( 'NONE', ( #33727 ), #67053, .F. ) ;
#60077=CARTESIAN_POINT ( 'NONE',  ( -25.49999999999981526, 6.052185695429106893, 5.000000000000000000 ) ) ;
#60078=DIRECTION ( 'NONE',  ( -0.000000000000000000, 0.3543493200069153248, 0.9351131265310292928 ) ) ;
#60080=ORIENTED_EDGE ( 'NONE', *, *, #130415, .T. ) ;
#60081=ORIENTED_EDGE ( 'NONE', *, *, #17324, .F. ) ;
#60082=ORIENTED_EDGE ( 'NONE', *, *, #104923, .F. ) ;
#60083=CARTESIAN_POINT ( 'NONE',  ( 0.000000000000000000, 0.000000000000000000, 5.000000000000000000 ) ) ;
#60084=FACE_OUTER_BOUND ( 'NONE', #132853, .T. ) ;
#60085=ADVANCED_FACE ( 'NONE', ( #1735 ), #93078, .F. ) ;
#60086=LINE ( 'NONE', #57250, #24214 ) ;
#60087=PLANE ( 'NONE',  #84343 ) ;
#60088=DIRECTION ( 'NONE',  ( 0.7071067811865487940, -0.7071067811865463515, 0.000000000000000000 ) ) ;
#60089=LINE ( 'NONE', #136917, #140627 ) ;
#60090=CARTESIAN_POINT ( 'NONE',  ( 26.67183060077628198, 5.259292476615659240, 4.000000000000000000 ) ) ;
#60091=DIRECTION ( 'NONE',  ( -0.7071067811865486830, -0.7071067811865464625, -0.000000000000000000 ) ) ;
#60092=DIRECTION ( 'NONE',  ( 0.6830127018922181881, 0.6830127018922202975, -0.2588190451025214056 ) ) ;
#60093=EDGE_LOOP ( 'NONE', ( #48653, #5891, #62298, #57860 ) ) ;
#60094=LINE ( 'NONE', #39037, #85749 ) ;
#60095=EDGE_CURVE ( 'NONE', #102270, #50596, #21825, .T. ) ;
#60096=VECTOR ( 'NONE', #67794, 1000.000000000000000 ) ;
#60097=CIRCLE ( 'NONE', #129500, 5.968999999999998529 ) ;
#60098=LINE ( 'NONE', #104268, #56377 ) ;
#60099=ORIENTED_EDGE ( 'NONE', *, *, #54477, .T. ) ;
#60100=AXIS2_PLACEMENT_3D ( 'NONE', #57021, #13449, #3297 ) ;
#60101=DIRECTION ( 'NONE',  ( 0.7071067811865487940, -0.7071067811865463515, 0.000000000000000000 ) ) ;
#60102=DIRECTION ( 'NONE',  ( -0.000000000000000000, -0.3543493200069152693, 0.9351131265310292928 ) ) ;
#60104=ORIENTED_EDGE ( 'NONE', *, *, #16978, .F. ) ;
#60105=LINE ( 'NONE', #51365, #132540 ) ;
#60107=DIRECTION ( 'NONE',  ( -0.6830127018922180770, -0.6830127018922204085, -0.2588190451025213501 ) ) ;
#60108=DIRECTION ( 'NONE',  ( -0.6830127018922181881, 0.6830127018922202975, -0.2588190451025214056 ) ) ;
#60109=ADVANCED_FACE ( 'NONE', ( #5328 ), #127115, .F. ) ;
#60112=VECTOR ( 'NONE', #73827, 1000.000000000000000 ) ;
#60113=ORIENTED_EDGE ( 'NONE', *, *, #140915, .T. ) ;
#60115=DIRECTION ( 'NONE',  ( -0.6830127018922181881, 0.6830127018922202975, -0.2588190451025214056 ) ) ;
#60116=ADVANCED_FACE ( 'NONE', ( #94486 ), #26404, .F. ) ;
#60118=CARTESIAN_POINT ( 'NONE',  ( -33.32816939922329880, 2.259292476615694323, 4.000000000000000000 ) ) ;
#60119=VECTOR ( 'NONE', #16541, 1000.000000000000000 ) ;
#60120=LINE ( 'NONE', #62981, #78648 ) ;
#60121=DIRECTION ( 'NONE',  ( 0.6830127018922181881, 0.6830127018922202975, -0.2588190451025214056 ) ) ;
#60122=DIRECTION ( 'NONE',  ( 0.7071067811865487940, 0.7071067811865463515, -0.000000000000000000 ) ) ;
#60123=CARTESIAN_POINT ( 'NONE',  ( 1.408325480989996326, -0.7407075233842770334, 14.76736230305380992 ) ) ;
#60126=VECTOR ( 'NONE', #7481, 1000.000000000000000 ) ;
#60128=AXIS2_PLACEMENT_3D ( 'NONE', #12387, #87815, #101537 ) ;
#60129=DIRECTION ( 'NONE',  ( 0.7071067811865487940, 0.7071067811865463515, 0.000000000000000000 ) ) ;
#60130=CARTESIAN_POINT ( 'NONE',  ( -60.48921356237309510, -27.52281430457097500, 5.000000000000000000 ) ) ;
#60131=ORIENTED_EDGE ( 'NONE', *, *, #62008, .T. ) ;
#60132=ORIENTED_EDGE ( 'NONE', *, *, #132094, .F. ) ;
#60134=VECTOR ( 'NONE', #133946, 999.9999999999998863 ) ;
#60135=ORIENTED_EDGE ( 'NONE', *, *, #15123, .T. ) ;
#60136=ORIENTED_EDGE ( 'NONE', *, *, #91505, .F. ) ;
#60138=LINE ( 'NONE', #16590, #20863 ) ;
#60139=CARTESIAN_POINT ( 'NONE',  ( 0.8124618758394703821, -22.22500000000000142, 4.000000000000000000 ) ) ;
#60141=AXIS2_PLACEMENT_3D ( 'NONE', #48049, #136454, #37154 ) ;
#60142=DIRECTION ( 'NONE',  ( -0.6830127018922180770, -0.6830127018922204085, -0.2588190451025213501 ) ) ;
#60145=VECTOR ( 'NONE', #108017, 1000.000000000000227 ) ;
#60146=DIRECTION ( 'NONE',  ( -0.7071067811865486830, -0.7071067811865464625, -0.000000000000000000 ) ) ;
#60148=VECTOR ( 'NONE', #137901, 1000.000000000000000 ) ;
#60149=DIRECTION ( 'NONE',  ( 0.7071067811865487940, 0.7071067811865463515, 0.000000000000000000 ) ) ;
#60150=CARTESIAN_POINT ( 'NONE',  ( 51.18398860626899705, 28.73617430169823095, 5.000000000000000000 ) ) ;
#60151=VECTOR ( 'NONE', #133076, 1000.000000000000000 ) ;
#60152=FACE_OUTER_BOUND ( 'NONE', #102668, .T. ) ;
#60153=CARTESIAN_POINT ( 'NONE',  ( -15.81246187583935914, -22.22500000000000142, 4.000000000000000000 ) ) ;
#60154=CARTESIAN_POINT ( 'NONE',  ( 13.11017322888201697, -22.22500000000000497, 4.785647885939354751 ) ) ;
#60155=DIRECTION ( 'NONE',  ( 0.7071067811865487940, 0.7071067811865463515, 0.000000000000000000 ) ) ;
#60156=PLANE ( 'NONE',  #102457 ) ;
#60157=ORIENTED_EDGE ( 'NONE', *, *, #114383, .F. ) ;
#60158=ORIENTED_EDGE ( 'NONE', *, *, #105621, .T. ) ;
#60160=ORIENTED_EDGE ( 'NONE', *, *, #20126, .F. ) ;
#60161=VECTOR ( 'NONE', #3533, 1000.000000000000000 ) ;
#60162=FACE_OUTER_BOUND ( 'NONE', #107882, .T. ) ;
#60163=VERTEX_POINT ( 'NONE', #105364 ) ;
#60164=CARTESIAN_POINT ( 'NONE',  ( 18.00548008471250583, 28.92564299267925776, 4.000000000000000000 ) ) ;
#60167=EDGE_LOOP ( 'NONE', ( #80879, #107152, #80739, #72709 ) ) ;
#60168=CARTESIAN_POINT ( 'NONE',  ( -13.08100000000000307, 3.174999999999997158, 5.000000000000000000 ) ) ;
#60169=VERTEX_POINT ( 'NONE', #38701 ) ;
#60170=CARTESIAN_POINT ( 'NONE',  ( -11.84387692260750136, -22.22500000000000497, 4.000000000000000000 ) ) ;
#60171=LINE ( 'NONE', #37709, #30668 ) ;
#60172=CARTESIAN_POINT ( 'NONE',  ( -24.59263130292903554, 0.9595543924999635488, 5.000000000000000000 ) ) ;
#60173=VERTEX_POINT ( 'NONE', #135871 ) ;
#60174=ORIENTED_EDGE ( 'NONE', *, *, #97573, .F. ) ;
#60175=EDGE_CURVE ( 'NONE', #128354, #70446, #27815, .T. ) ;
#60176=ORIENTED_EDGE ( 'NONE', *, *, #136558, .T. ) ;
#60177=DIRECTION ( 'NONE',  ( -0.7071067811865486830, -0.7071067811865464625, 0.000000000000000000 ) ) ;
#60178=ADVANCED_FACE ( 'NONE', ( #80786 ), #48873, .F. ) ;
#60179=DIRECTION ( 'NONE',  ( -0.3543493200069162685, -0.000000000000000000, -0.9351131265310288487 ) ) ;
#60182=VERTEX_POINT ( 'NONE', #93790 ) ;
#60184=VERTEX_POINT ( 'NONE', #38006 ) ;
#60185=FACE_OUTER_BOUND ( 'NONE', #47413, .T. ) ;
#60187=ORIENTED_EDGE ( 'NONE', *, *, #13506, .F. ) ;
#60188=DIRECTION ( 'NONE',  ( 0.3543493200069162685, -0.000000000000000000, -0.9351131265310288487 ) ) ;
#60189=EDGE_CURVE ( 'NONE', #24896, #106536, #36551, .T. ) ;
#60190=VECTOR ( 'NONE', #68641, 999.9999999999998863 ) ;
#60191=DIRECTION ( 'NONE',  ( 1.000000000000000000, 0.000000000000000000, 0.000000000000000000 ) ) ;
#60192=CARTESIAN_POINT ( 'NONE',  ( 34.49999999999976552, 3.073033219394661675, -6.593910359670890564 ) ) ;
#60195=CARTESIAN_POINT ( 'NONE',  ( -26.99999999999982236, -2.904428200921339354, -6.989807076074882275 ) ) ;
#60196=VECTOR ( 'NONE', #125489, 1000.000000000000227 ) ;
#60197=ADVANCED_FACE ( 'NONE', ( #3198 ), #82232, .F. ) ;
#60198=VECTOR ( 'NONE', #9946, 1000.000000000000000 ) ;
#60199=( BOUNDED_CURVE ( )  B_SPLINE_CURVE ( 3, ( #135103, #121322, #90122, #67710 ),
 .UNSPECIFIED., .F., .T. ) 
 B_SPLINE_CURVE_WITH_KNOTS ( ( 4, 4 ),
 ( 4.517163242187656635, 4.562733109340372906 ),
 .UNSPECIFIED. ) 
 CURVE ( )  GEOMETRIC_REPRESENTATION_ITEM ( )  RATIONAL_B_SPLINE_CURVE ( ( 1.000000000000000000, 0.9998269564205118920, 0.9998269564205118920, 1.000000000000000000 ) ) 
 REPRESENTATION_ITEM ( '' )  );
#60200=DIRECTION ( 'NONE',  ( -0.3543493200069162685, -0.000000000000000000, -0.9351131265310288487 ) ) ;
#60201=AXIS2_PLACEMENT_3D ( 'NONE', #53226, #64848, #66989 ) ;
#60202=CARTESIAN_POINT ( 'NONE',  ( 23.99451991528749062, 28.92564299267954908, 4.000000000000000000 ) ) ;
#60203=FACE_BOUND ( 'NONE', #49266, .T. ) ;
#60204=ORIENTED_EDGE ( 'NONE', *, *, #70681, .T. ) ;
#60205=DIRECTION ( 'NONE',  ( 0.7071067811865487940, 0.7071067811865463515, 0.000000000000000000 ) ) ;
#60206=CARTESIAN_POINT ( 'NONE',  ( -75.48921356237309510, -27.52281430457107803, 5.000000000000000000 ) ) ;
#60208=ORIENTED_EDGE ( 'NONE', *, *, #79733, .F. ) ;
#60210=ORIENTED_EDGE ( 'NONE', *, *, #32857, .F. ) ;
#60211=EDGE_CURVE ( 'NONE', #26318, #44215, #83661, .T. ) ;
#60213=VECTOR ( 'NONE', #49797, 999.9999999999998863 ) ;
#60216=ORIENTED_EDGE ( 'NONE', *, *, #235, .F. ) ;
#60217=CARTESIAN_POINT ( 'NONE',  ( 21.48921356237309155, -27.52281430457070499, 5.000000000000000000 ) ) ;
#60218=LINE ( 'NONE', #5061, #138741 ) ;
#60219=DIRECTION ( 'NONE',  ( 0.3543493200069162685, -0.000000000000000000, -0.9351131265310288487 ) ) ;
#60220=EDGE_CURVE ( 'NONE', #63482, #89870, #14797, .T. ) ;
#60221=ORIENTED_EDGE ( 'NONE', *, *, #108255, .F. ) ;
#60222=CARTESIAN_POINT ( 'NONE',  ( -45.18398860626900415, 28.73617430169818832, 5.000000000000000000 ) ) ;
#60224=VECTOR ( 'NONE', #119108, 1000.000000000000000 ) ;
#60225=AXIS2_PLACEMENT_3D ( 'NONE', #31309, #62522, #108108 ) ;
#60226=DIRECTION ( 'NONE',  ( 0.000000000000000000, -0.3543493200069153248, -0.9351131265310291818 ) ) ;
#60228=EDGE_CURVE ( 'NONE', #22767, #87580, #57852, .T. ) ;
#60229=VECTOR ( 'NONE', #101133, 1000.000000000000000 ) ;
#60231=DIRECTION ( 'NONE',  ( -0.000000000000000000, 0.3543493200069153248, 0.9351131265310292928 ) ) ;
#60232=LINE ( 'NONE', #139936, #22799 ) ;
#60233=DIRECTION ( 'NONE',  ( -0.000000000000000000, 0.000000000000000000, 1.000000000000000000 ) ) ;
#60234=ORIENTED_EDGE ( 'NONE', *, *, #98211, .F. ) ;
#60237=ORIENTED_EDGE ( 'NONE', *, *, #44337, .F. ) ;
#60238=EDGE_LOOP ( 'NONE', ( #104099, #113786, #98854, #23575 ) ) ;
#60239=DIRECTION ( 'NONE',  ( 1.000000000000000000, 0.000000000000000000, 0.000000000000000000 ) ) ;
#60240=ORIENTED_EDGE ( 'NONE', *, *, #128865, .T. ) ;
#60241=EDGE_CURVE ( 'NONE', #78067, #22380, #129988, .T. ) ;
#60243=DIRECTION ( 'NONE',  ( -0.7071067811865486830, 0.7071067811865464625, 0.000000000000000000 ) ) ;
#60244=ADVANCED_FACE ( 'NONE', ( #40839 ), #19783, .F. ) ;
#60246=EDGE_CURVE ( 'NONE', #123521, #105758, #106056, .T. ) ;
#60247=CARTESIAN_POINT ( 'NONE',  ( -34.92500000000001137, -19.29806943317879586, 4.500000000000000888 ) ) ;
#60248=ORIENTED_EDGE ( 'NONE', *, *, #121353, .F. ) ;
#60250=CARTESIAN_POINT ( 'NONE',  ( -33.29974487139158867, -27.71228299555229313, 4.000000000000000000 ) ) ;
#60251=ORIENTED_EDGE ( 'NONE', *, *, #38549, .T. ) ;
#60252=LINE ( 'NONE', #104427, #53663 ) ;
#60255=VERTEX_POINT ( 'NONE', #42994 ) ;
#60257=CARTESIAN_POINT ( 'NONE',  ( -0.2800196798940397525, 0.7592924766157104211, 14.27032725228008836 ) ) ;
#60258=EDGE_CURVE ( 'NONE', #76705, #15400, #136679, .T. ) ;
#60260=LINE ( 'NONE', #29035, #90604 ) ;
#60262=ORIENTED_EDGE ( 'NONE', *, *, #63416, .T. ) ;
#60263=DIRECTION ( 'NONE',  ( -0.3543493200069162685, -0.000000000000000000, -0.9351131265310288487 ) ) ;
#60264=ORIENTED_EDGE ( 'NONE', *, *, #98636, .T. ) ;
#60266=CARTESIAN_POINT ( 'NONE',  ( -2.287690060339689690, -21.73547319004780931, 4.999917730833664642 ) ) ;
#60267=DIRECTION ( 'NONE',  ( 0.7071067811865487940, 0.7071067811865463515, 0.000000000000000000 ) ) ;
#60268=PLANE ( 'NONE',  #98594 ) ;
#60270=CARTESIAN_POINT ( 'NONE',  ( 84.48921356237309510, -27.52281430457114197, 5.000000000000000000 ) ) ;
#60271=DIRECTION ( 'NONE',  ( 0.7071067811865487940, 0.7071067811865463515, -0.000000000000000000 ) ) ;
#60272=VERTEX_POINT ( 'NONE', #86496 ) ;
#60273=CARTESIAN_POINT ( 'NONE',  ( 36.29974487139159578, -27.71228299555231445, 4.000000000000000000 ) ) ;
#60274=CARTESIAN_POINT ( 'NONE',  ( 34.42499999999998295, 0.000000000000000000, 0.000000000000000000 ) ) ;
#60275=LINE ( 'NONE', #71868, #30666 ) ;
#60276=VERTEX_POINT ( 'NONE', #75614 ) ;
#60277=LINE ( 'NONE', #28349, #32738 ) ;
#60279=FACE_OUTER_BOUND ( 'NONE', #15621, .T. ) ;
#60281=FACE_OUTER_BOUND ( 'NONE', #88161, .T. ) ;
#60282=ORIENTED_EDGE ( 'NONE', *, *, #46669, .T. ) ;
#60285=CARTESIAN_POINT ( 'NONE',  ( -34.92500000000001137, -19.29806943317879586, 4.500000000000000888 ) ) ;
#60286=VECTOR ( 'NONE', #131609, 1000.000000000000000 ) ;
#60287=ORIENTED_EDGE ( 'NONE', *, *, #131479, .F. ) ;
#60288=LINE ( 'NONE', #93612, #95141 ) ;
#60290=EDGE_CURVE ( 'NONE', #50064, #86945, #117643, .T. ) ;
#60291=LINE ( 'NONE', #62425, #75323 ) ;
#60292=ADVANCED_FACE ( 'NONE', ( #140837 ), #9602, .T. ) ;
#60293=DIRECTION ( 'NONE',  ( -0.7071067811865487940, 0.7071067811865463515, -0.000000000000000000 ) ) ;
#60294=ORIENTED_EDGE ( 'NONE', *, *, #120268, .T. ) ;
#60295=DIRECTION ( 'NONE',  ( 0.7071067811865487940, 0.7071067811865463515, 0.000000000000000000 ) ) ;
#60296=DIRECTION ( 'NONE',  ( -0.7071067811865487940, 0.7071067811865463515, -0.000000000000000000 ) ) ;
#60298=CARTESIAN_POINT ( 'NONE',  ( -48.18398860626899705, 28.73617430169820608, 5.000000000000000000 ) ) ;
#60299=CARTESIAN_POINT ( 'NONE',  ( -24.48921356237309510, -27.52281430457072631, 5.000000000000000000 ) ) ;
#60300=DIRECTION ( 'NONE',  ( 0.7071067811865486830, -0.7071067811865464625, -0.000000000000000000 ) ) ;
#60301=DIRECTION ( 'NONE',  ( 1.000000000000000000, 0.000000000000000000, 0.000000000000000000 ) ) ;
#60302=LINE ( 'NONE', #137130, #22214 ) ;
#60303=EDGE_LOOP ( 'NONE', ( #93382, #18190, #113443 ) ) ;
#60304=VERTEX_POINT ( 'NONE', #30693 ) ;
#60305=ORIENTED_EDGE ( 'NONE', *, *, #94390, .T. ) ;
#60308=AXIS2_PLACEMENT_3D ( 'NONE', #31459, #30757, #74249 ) ;
#60309=ORIENTED_EDGE ( 'NONE', *, *, #93283, .F. ) ;
#60310=ORIENTED_EDGE ( 'NONE', *, *, #64921, .T. ) ;
#60311=ORIENTED_EDGE ( 'NONE', *, *, #94469, .F. ) ;
#60312=AXIS2_PLACEMENT_3D ( 'NONE', #140058, #38586, #129876 ) ;
#60315=VECTOR ( 'NONE', #21751, 1000.000000000000227 ) ;
#60317=VERTEX_POINT ( 'NONE', #74922 ) ;
#60318=DIRECTION ( 'NONE',  ( 0.7071067811865486830, -0.7071067811865464625, -0.000000000000000000 ) ) ;
#60319=VECTOR ( 'NONE', #33849, 1000.000000000000000 ) ;
#60320=LINE ( 'NONE', #69780, #34797 ) ;
#60321=DIRECTION ( 'NONE',  ( -0.000000000000000000, 0.000000000000000000, 1.000000000000000000 ) ) ;
#60323=VERTEX_POINT ( 'NONE', #7469 ) ;
#60324=DIRECTION ( 'NONE',  ( 0.3543493200069163240, 0.000000000000000000, -0.9351131265310288487 ) ) ;
#60325=PLANE ( 'NONE',  #130348 ) ;
#60326=CARTESIAN_POINT ( 'NONE',  ( -30.71230993966007716, -21.73547319004781286, 4.999917730833664642 ) ) ;
#60327=AXIS2_PLACEMENT_3D ( 'NONE', #79788, #58755, #70337 ) ;
#60328=CARTESIAN_POINT ( 'NONE',  ( 0.000000000000000000, 0.000000000000000000, 5.000000000000000000 ) ) ;
#60329=DIRECTION ( 'NONE',  ( 0.7071067811865487940, 0.7071067811865463515, -0.000000000000000000 ) ) ;
#60332=FACE_OUTER_BOUND ( 'NONE', #129686, .T. ) ;
#60333=ORIENTED_EDGE ( 'NONE', *, *, #105114, .T. ) ;
#60334=ORIENTED_EDGE ( 'NONE', *, *, #28115, .T. ) ;
#60336=ORIENTED_EDGE ( 'NONE', *, *, #41539, .F. ) ;
#60337=EDGE_LOOP ( 'NONE', ( #13652, #51085, #93754, #130257 ) ) ;
#60338=CARTESIAN_POINT ( 'NONE',  ( 0.000000000000000000, 0.000000000000000000, 5.000000000000000000 ) ) ;
#60339=LINE ( 'NONE', #126284, #80251 ) ;
#60340=ORIENTED_EDGE ( 'NONE', *, *, #48125, .F. ) ;
#60341=FACE_OUTER_BOUND ( 'NONE', #140307, .T. ) ;
#60343=CARTESIAN_POINT ( 'NONE',  ( 66.48921356237309510, -27.52281430457101763, 5.000000000000000000 ) ) ;
#60344=VECTOR ( 'NONE', #91226, 1000.000000000000000 ) ;
#60347=EDGE_LOOP ( 'NONE', ( #85366, #4691, #105284, #133215 ) ) ;
#60348=AXIS2_PLACEMENT_3D ( 'NONE', #119118, #109673, #130005 ) ;
#60349=LINE ( 'NONE', #59638, #31762 ) ;
#60350=VERTEX_POINT ( 'NONE', #108192 ) ;
#60352=VECTOR ( 'NONE', #84373, 1000.000000000000000 ) ;
#60353=DIRECTION ( 'NONE',  ( -0.7071067811865486830, -0.7071067811865464625, 0.000000000000000000 ) ) ;
#60354=DIRECTION ( 'NONE',  ( 0.7071067811865487940, 0.7071067811865463515, 0.000000000000000000 ) ) ;
#60355=EDGE_CURVE ( 'NONE', #42461, #18811, #97598, .T. ) ;
#60356=PLANE ( 'NONE',  #125197 ) ;
#60357=ORIENTED_EDGE ( 'NONE', *, *, #17579, .T. ) ;
#60359=EDGE_CURVE ( 'NONE', #121292, #89747, #97315, .T. ) ;
#60364=LINE ( 'NONE', #14690, #8321 ) ;
#60365=CARTESIAN_POINT ( 'NONE',  ( 10.49999999999993605, -2.173586137069121627, -4.605770156576090457 ) ) ;
#60366=EDGE_CURVE ( 'NONE', #108894, #104436, #17628, .T. ) ;
#60367=EDGE_CURVE ( 'NONE', #43828, #72705, #31392, .T. ) ;
#60368=VECTOR ( 'NONE', #44628, 1000.000000000000000 ) ;
#60370=ORIENTED_EDGE ( 'NONE', *, *, #127772, .T. ) ;
#60372=EDGE_CURVE ( 'NONE', #127035, #16309, #20482, .T. ) ;
#60373=LINE ( 'NONE', #104553, #57235 ) ;
#60374=VERTEX_POINT ( 'NONE', #95923 ) ;
#60375=ORIENTED_EDGE ( 'NONE', *, *, #48896, .T. ) ;
#60376=VECTOR ( 'NONE', #86343, 999.9999999999998863 ) ;
#60377=LINE ( 'NONE', #137208, #35436 ) ;
#60378=ORIENTED_EDGE ( 'NONE', *, *, #37913, .F. ) ;
#60379=EDGE_CURVE ( 'NONE', #43144, #133750, #112513, .T. ) ;
#60380=FACE_OUTER_BOUND ( 'NONE', #85164, .T. ) ;
#60381=ORIENTED_EDGE ( 'NONE', *, *, #11903, .F. ) ;
#60382=DIRECTION ( 'NONE',  ( -0.7071067811865487940, 0.7071067811865463515, 0.000000000000000000 ) ) ;
#60383=AXIS2_PLACEMENT_3D ( 'NONE', #16714, #68981, #17421 ) ;
#60385=LINE ( 'NONE', #81431, #132260 ) ;
#60386=FACE_BOUND ( 'NONE', #32102, .T. ) ;
#60388=CARTESIAN_POINT ( 'NONE',  ( -42.48921356237308800, -27.52281430457085065, 5.000000000000000000 ) ) ;
#60389=DIRECTION ( 'NONE',  ( -0.000000000000000000, 0.3543493200069153248, 0.9351131265310292928 ) ) ;
#60392=ORIENTED_EDGE ( 'NONE', *, *, #94086, .F. ) ;
#60393=EDGE_CURVE ( 'NONE', #134254, #11791, #56029, .T. ) ;
#60394=AXIS2_PLACEMENT_3D ( 'NONE', #111828, #54597, #143016 ) ;
#60395=DIRECTION ( 'NONE',  ( 0.7071067811865487940, -0.7071067811865463515, 0.000000000000000000 ) ) ;
#60396=EDGE_LOOP ( 'NONE', ( #128323, #108763, #28601, #102253 ) ) ;
#60397=VERTEX_POINT ( 'NONE', #21928 ) ;
#60399=ORIENTED_EDGE ( 'NONE', *, *, #92964, .T. ) ;
#60400=CARTESIAN_POINT ( 'NONE',  ( -29.99999999999978684, -3.485240976185105310, -4.108735105802465704 ) ) ;
#60401=EDGE_CURVE ( 'NONE', #136233, #46484, #56756, .T. ) ;
#60402=ORIENTED_EDGE ( 'NONE', *, *, #102224, .F. ) ;
#60404=VECTOR ( 'NONE', #61038, 1000.000000000000000 ) ;
#60407=VECTOR ( 'NONE', #131484, 999.9999999999998863 ) ;
#60408=CARTESIAN_POINT ( 'NONE',  ( -29.99999999999979039, 7.007997736742422212, -8.085015511992182269 ) ) ;
#60409=DIRECTION ( 'NONE',  ( -0.000000000000000000, 0.000000000000000000, 1.000000000000000000 ) ) ;
#60410=PLANE ( 'NONE',  #115304 ) ;
#60411=EDGE_CURVE ( 'NONE', #35909, #48454, #869, .T. ) ;
#60412=DIRECTION ( 'NONE',  ( -0.7071067811865486830, -0.7071067811865464625, 0.000000000000000000 ) ) ;
#60413=FACE_OUTER_BOUND ( 'NONE', #124529, .T. ) ;
#60414=ORIENTED_EDGE ( 'NONE', *, *, #106144, .T. ) ;
#60416=VECTOR ( 'NONE', #73636, 999.9999999999998863 ) ;
#60417=EDGE_LOOP ( 'NONE', ( #96692, #20169, #104112, #112586 ) ) ;
#60418=VECTOR ( 'NONE', #121808, 1000.000000000000000 ) ;
#60420=DIRECTION ( 'NONE',  ( -1.000000000000000000, -7.992108492102899539E-15, 0.000000000000000000 ) ) ;
#60421=ORIENTED_EDGE ( 'NONE', *, *, #123223, .F. ) ;
#60423=VECTOR ( 'NONE', #65050, 1000.000000000000000 ) ;
#60424=ORIENTED_EDGE ( 'NONE', *, *, #141234, .T. ) ;
#60425=ORIENTED_EDGE ( 'NONE', *, *, #38820, .F. ) ;
#60426=PLANE ( 'NONE',  #72158 ) ;
#60429=AXIS2_PLACEMENT_3D ( 'NONE', #46257, #134685, #68706 ) ;
#60430=DIRECTION ( 'NONE',  ( -0.7071067811865487940, 0.7071067811865463515, 0.000000000000000000 ) ) ;
#60431=LINE ( 'NONE', #29189, #67877 ) ;
#60433=CARTESIAN_POINT ( 'NONE',  ( 5.671830600776438303, 11.25929247661560950, 4.000000000000000000 ) ) ;
#60434=ORIENTED_EDGE ( 'NONE', *, *, #8369, .F. ) ;
#60435=AXIS2_PLACEMENT_3D ( 'NONE', #948, #100990, #47390 ) ;
#60436=EDGE_CURVE ( 'NONE', #128691, #103116, #123423, .T. ) ;
#60437=CARTESIAN_POINT ( 'NONE',  ( 9.722814304570524868, -21.72500000000000497, 5.000000000000000000 ) ) ;
#60438=PLANE ( 'NONE',  #4863 ) ;
#60440=LINE ( 'NONE', #82195, #112280 ) ;
#60441=CARTESIAN_POINT ( 'NONE',  ( 17.70025512860841488, -27.71228299555193786, 4.000000000000000000 ) ) ;
#60442=ORIENTED_EDGE ( 'NONE', *, *, #99245, .T. ) ;
#60444=VERTEX_POINT ( 'NONE', #13170 ) ;
#60445=CARTESIAN_POINT ( 'NONE',  ( -8.999999999999932498, 14.87792677143808362, -11.06722581663441929 ) ) ;
#60447=CARTESIAN_POINT ( 'NONE',  ( 0.000000000000000000, 0.000000000000000000, 5.000000000000000000 ) ) ;
#60449=VERTEX_POINT ( 'NONE', #46600 ) ;
#60451=VECTOR ( 'NONE', #39477, 999.9999999999998863 ) ;
#60452=DIRECTION ( 'NONE',  ( -0.6830127018922181881, 0.6830127018922202975, -0.2588190451025214056 ) ) ;
#60454=CARTESIAN_POINT ( 'NONE',  ( -30.48921356237309510, -27.52281430457076894, 5.000000000000000000 ) ) ;
#60455=ORIENTED_EDGE ( 'NONE', *, *, #97347, .T. ) ;
#60456=DIRECTION ( 'NONE',  ( -0.000000000000000000, 0.000000000000000000, 1.000000000000000000 ) ) ;
#60458=CARTESIAN_POINT ( 'NONE',  ( 2.816011393730999401, 28.73617430169785436, 5.000000000000000000 ) ) ;
#60459=DIRECTION ( 'NONE',  ( 0.3543493200069162685, -0.000000000000000000, -0.9351131265310288487 ) ) ;
#60461=CARTESIAN_POINT ( 'NONE',  ( 12.48921356237309155, -27.52281430457064104, 5.000000000000000000 ) ) ;
#60462=ORIENTED_EDGE ( 'NONE', *, *, #36474, .F. ) ;
#60463=ADVANCED_FACE ( 'NONE', ( #24085 ), #78470, .F. ) ;
#60468=DIRECTION ( 'NONE',  ( 0.7071067811865486830, -0.7071067811865464625, -0.000000000000000000 ) ) ;
#60469=ADVANCED_FACE ( 'NONE', ( #44439 ), #57444, .T. ) ;
#60470=VECTOR ( 'NONE', #15717, 1000.000000000000000 ) ;
#60471=FACE_OUTER_BOUND ( 'NONE', #105493, .T. ) ;
#60472=CARTESIAN_POINT ( 'NONE',  ( 34.47516574401890210, -13.50948238788423872, 4.998110765256833510 ) ) ;
#60473=DIRECTION ( 'NONE',  ( 0.7071067811865487940, -0.7071067811865463515, 0.000000000000000000 ) ) ;
#60474=ORIENTED_EDGE ( 'NONE', *, *, #28660, .F. ) ;
#60475=CARTESIAN_POINT ( 'NONE',  ( 2.816011393730999401, 28.73617430169785436, 5.000000000000000000 ) ) ;
#60476=VECTOR ( 'NONE', #55513, 1000.000000000000000 ) ;
#60478=VECTOR ( 'NONE', #109285, 1000.000000000000000 ) ;
#60481=EDGE_CURVE ( 'NONE', #66027, #52394, #89334, .T. ) ;
#60482=DIRECTION ( 'NONE',  ( 0.6830127018922181881, 0.6830127018922202975, -0.2588190451025214056 ) ) ;
#60484=EDGE_LOOP ( 'NONE', ( #79267, #36427, #82666, #1603 ) ) ;
#60486=VERTEX_POINT ( 'NONE', #21219 ) ;
#60487=ORIENTED_EDGE ( 'NONE', *, *, #91855, .T. ) ;
#60488=DIRECTION ( 'NONE',  ( -0.6830127018922180770, -0.6830127018922204085, -0.2588190451025213501 ) ) ;
#60489=CARTESIAN_POINT ( 'NONE',  ( 60.18398860626900415, 28.73617430169829490, 5.000000000000000000 ) ) ;
#60490=DIRECTION ( 'NONE',  ( 0.3543493200069162685, -0.000000000000000000, -0.9351131265310288487 ) ) ;
#60491=LINE ( 'NONE', #70660, #99430 ) ;
#60492=ADVANCED_FACE ( 'NONE', ( #32840 ), #143001, .F. ) ;
#60493=CARTESIAN_POINT ( 'NONE',  ( -34.92500000000001137, -16.29806943317882073, 4.500000000000000888 ) ) ;
#60494=FACE_OUTER_BOUND ( 'NONE', #113053, .T. ) ;
#60495=EDGE_LOOP ( 'NONE', ( #87946, #110865, #115460, #12506 ) ) ;
#60496=CARTESIAN_POINT ( 'NONE',  ( 9.489213562373095101, -27.52281430457062328, 5.000000000000000000 ) ) ;
#60497=CARTESIAN_POINT ( 'NONE',  ( -29.20710678118633297, -20.24070752338407075, 5.000000000000000000 ) ) ;
#60500=DIRECTION ( 'NONE',  ( 0.3543493200069162685, -0.000000000000000000, -0.9351131265310288487 ) ) ;
#60501=DIRECTION ( 'NONE',  ( -0.7071067811865486830, 0.7071067811865464625, 0.000000000000000000 ) ) ;
#60502=LINE ( 'NONE', #104679, #13276 ) ;
#60504=LINE ( 'NONE', #50321, #73878 ) ;
#60505=VERTEX_POINT ( 'NONE', #122661 ) ;
#60506=ORIENTED_EDGE ( 'NONE', *, *, #58024, .F. ) ;
#60508=FACE_OUTER_BOUND ( 'NONE', #92886, .T. ) ;
#60510=CARTESIAN_POINT ( 'NONE',  ( -2.510786437626908008, -27.52281430457053446, 5.000000000000000000 ) ) ;
#60511=VERTEX_POINT ( 'NONE', #10328 ) ;
#60513=VECTOR ( 'NONE', #7008, 1000.000000000000000 ) ;
#60514=AXIS2_PLACEMENT_3D ( 'NONE', #102069, #112935, #14343 ) ;
#60517=EDGE_CURVE ( 'NONE', #99825, #7978, #54583, .T. ) ;
#60519=VERTEX_POINT ( 'NONE', #11742 ) ;
#60520=VECTOR ( 'NONE', #107310, 999.9999999999998863 ) ;
#60521=VERTEX_POINT ( 'NONE', #137 ) ;
#60522=VECTOR ( 'NONE', #53128, 999.9999999999998863 ) ;
#60523=AXIS2_PLACEMENT_3D ( 'NONE', #82560, #126750, #62247 ) ;
#60524=VECTOR ( 'NONE', #139150, 1000.000000000000000 ) ;
#60525=CARTESIAN_POINT ( 'NONE',  ( -60.48921356237309510, -27.52281430457097500, 5.000000000000000000 ) ) ;
#60527=LINE ( 'NONE', #51774, #128713 ) ;
#60528=CARTESIAN_POINT ( 'NONE',  ( -42.48921356237308800, -27.52281430457085065, 5.000000000000000000 ) ) ;
#60530=CARTESIAN_POINT ( 'NONE',  ( -15.67180000000000639, 3.174999999999997158, 5.000000000000000000 ) ) ;
#60533=LINE ( 'NONE', #93834, #91548 ) ;
#60534=ORIENTED_EDGE ( 'NONE', *, *, #50171, .T. ) ;
#60535=CARTESIAN_POINT ( 'NONE',  ( -1.499999999999987566, -4.216083040037250207, -7.486842126848652690 ) ) ;
#60536=FACE_OUTER_BOUND ( 'NONE', #124604, .T. ) ;
#60537=CARTESIAN_POINT ( 'NONE',  ( 6.005480084712508493, 28.92564299267933947, 4.000000000000000000 ) ) ;
#60539=DIRECTION ( 'NONE',  ( 0.7071067811865487940, 0.7071067811865463515, 0.000000000000000000 ) ) ;
#60540=EDGE_CURVE ( 'NONE', #45681, #37108, #16766, .T. ) ;
#60542=EDGE_CURVE ( 'NONE', #143176, #12388, #51472, .T. ) ;
#60544=EDGE_CURVE ( 'NONE', #51106, #140375, #16016, .T. ) ;
#60546=LINE ( 'NONE', #104718, #126398 ) ;
#60547=LINE ( 'NONE', #80854, #125156 ) ;
#60549=CARTESIAN_POINT ( 'NONE',  ( 0.000000000000000000, 0.000000000000000000, 5.000000000000000000 ) ) ;
#60550=ORIENTED_EDGE ( 'NONE', *, *, #29927, .T. ) ;
#60552=ADVANCED_FACE ( 'NONE', ( #92168 ), #81340, .F. ) ;
#60553=CARTESIAN_POINT ( 'NONE',  ( -2.999999999999979128, 19.55218569542897100, 5.000000000000000000 ) ) ;
#60557=ORIENTED_EDGE ( 'NONE', *, *, #47032, .F. ) ;
#60558=AXIS2_PLACEMENT_3D ( 'NONE', #94184, #105759, #41236 ) ;
#60559=LINE ( 'NONE', #28629, #16624 ) ;
#60560=ORIENTED_EDGE ( 'NONE', *, *, #101580, .T. ) ;
#60561=VECTOR ( 'NONE', #56339, 1000.000000000000000 ) ;
#60562=DIRECTION ( 'NONE',  ( 1.000000000000000000, 0.000000000000000000, 0.000000000000000000 ) ) ;
#60564=AXIS2_PLACEMENT_3D ( 'NONE', #140507, #62989, #41194 ) ;
#60566=FACE_BOUND ( 'NONE', #9902, .T. ) ;
#60567=VECTOR ( 'NONE', #46594, 1000.000000000000000 ) ;
#60570=CARTESIAN_POINT ( 'NONE',  ( 34.42499999999998295, -6.022814304570537125, 5.000000000000000000 ) ) ;
#60571=LINE ( 'NONE', #5406, #138537 ) ;
#60572=LINE ( 'NONE', #40238, #57423 ) ;
#60573=ORIENTED_EDGE ( 'NONE', *, *, #111323, .F. ) ;
#60574=EDGE_CURVE ( 'NONE', #94828, #125282, #35711, .T. ) ;
#60575=DIRECTION ( 'NONE',  ( -0.000000000000000000, 0.000000000000000000, 1.000000000000000000 ) ) ;
#60578=ORIENTED_EDGE ( 'NONE', *, *, #113531, .T. ) ;
#60581=FACE_OUTER_BOUND ( 'NONE', #119079, .T. ) ;
#60582=VECTOR ( 'NONE', #78336, 999.9999999999998863 ) ;
#60583=DIRECTION ( 'NONE',  ( -0.7071067811865487940, 0.7071067811865463515, 0.000000000000000000 ) ) ;
#60584=VECTOR ( 'NONE', #79929, 999.9999999999998863 ) ;
#60585=CARTESIAN_POINT ( 'NONE',  ( 21.87889065874226091, 8.431076354171498366, 5.000000000000000000 ) ) ;
#60586=PLANE ( 'NONE',  #109573 ) ;
#60587=EDGE_CURVE ( 'NONE', #13630, #22921, #58908, .T. ) ;
#60588=VERTEX_POINT ( 'NONE', #102376 ) ;
#60590=CARTESIAN_POINT ( 'NONE',  ( 0.000000000000000000, 0.000000000000000000, 5.000000000000000000 ) ) ;
#60591=PLANE ( 'NONE',  #64315 ) ;
#60592=VECTOR ( 'NONE', #141901, 1000.000000000000227 ) ;
#60593=DIRECTION ( 'NONE',  ( -0.6830127018922181881, 0.6830127018922202975, -0.2588190451025214056 ) ) ;
#60594=CARTESIAN_POINT ( 'NONE',  ( 35.99451991528749772, 28.92564299267963079, 4.000000000000000000 ) ) ;
#60596=FACE_OUTER_BOUND ( 'NONE', #107493, .T. ) ;
#60597=DIRECTION ( 'NONE',  ( 0.6830127018922181881, 0.6830127018922202975, -0.2588190451025214056 ) ) ;
#60599=DIRECTION ( 'NONE',  ( 0.3543493200069163240, -0.000000000000000000, 0.9351131265310288487 ) ) ;
#60600=ORIENTED_EDGE ( 'NONE', *, *, #25058, .T. ) ;
#60601=DIRECTION ( 'NONE',  ( -0.6830127018922180770, -0.6830127018922204085, -0.2588190451025213501 ) ) ;
#60602=EDGE_CURVE ( 'NONE', #47430, #140430, #91489, .T. ) ;
#60603=LINE ( 'NONE', #49714, #30365 ) ;
#60604=VERTEX_POINT ( 'NONE', #26227 ) ;
#60605=EDGE_LOOP ( 'NONE', ( #97324, #121088, #3306, #132034 ) ) ;
#60606=ORIENTED_EDGE ( 'NONE', *, *, #84406, .T. ) ;
#60608=AXIS2_PLACEMENT_3D ( 'NONE', #35195, #125022, #11970 ) ;
#60609=ORIENTED_EDGE ( 'NONE', *, *, #12251, .T. ) ;
#60612=VERTEX_POINT ( 'NONE', #36387 ) ;
#60613=ADVANCED_FACE ( 'NONE', ( #80617 ), #124816, .F. ) ;
#60615=ORIENTED_EDGE ( 'NONE', *, *, #63238, .T. ) ;
#60617=VECTOR ( 'NONE', #95366, 1000.000000000000000 ) ;
#60618=VECTOR ( 'NONE', #116011, 1000.000000000000000 ) ;
#60619=LINE ( 'NONE', #5451, #109551 ) ;
#60620=ORIENTED_EDGE ( 'NONE', *, *, #84945, .T. ) ;
#60621=EDGE_LOOP ( 'NONE', ( #132120, #130417, #73130, #109347 ) ) ;
#60622=( BOUNDED_CURVE ( )  B_SPLINE_CURVE ( 3, ( #19386, #10629, #143304, #141151 ),
 .UNSPECIFIED., .F., .F. ) 
 B_SPLINE_CURVE_WITH_KNOTS ( ( 4, 4 ),
 ( 2.779374508378133601, 4.199602562396795413 ),
 .UNSPECIFIED. ) 
 CURVE ( )  GEOMETRIC_REPRESENTATION_ITEM ( )  RATIONAL_B_SPLINE_CURVE ( ( 1.000000000000000000, 0.8388583629366719308, 0.8388583629366719308, 1.000000000000000000 ) ) 
 REPRESENTATION_ITEM ( '' )  );
#60623=LINE ( 'NONE', #38834, #60832 ) ;
#60625=AXIS2_PLACEMENT_3D ( 'NONE', #80043, #124218, #24894 ) ;
#60626=VECTOR ( 'NONE', #91723, 1000.000000000000114 ) ;
#60627=ORIENTED_EDGE ( 'NONE', *, *, #13522, .F. ) ;
#60628=DIRECTION ( 'NONE',  ( -0.7071067811865486830, -0.7071067811865464625, 0.000000000000000000 ) ) ;
#60629=VERTEX_POINT ( 'NONE', #70490 ) ;
#60630=VERTEX_POINT ( 'NONE', #4392 ) ;
#60632=ORIENTED_EDGE ( 'NONE', *, *, #66247, .T. ) ;
#60633=ORIENTED_EDGE ( 'NONE', *, *, #46227, .T. ) ;
#60634=DIRECTION ( 'NONE',  ( -0.3543493200069162685, -0.000000000000000000, -0.9351131265310288487 ) ) ;
#60635=VECTOR ( 'NONE', #119266, 1000.000000000000000 ) ;
#60636=AXIS2_PLACEMENT_3D ( 'NONE', #43702, #45171, #58201 ) ;
#60637=AXIS2_PLACEMENT_3D ( 'NONE', #134474, #133063, #131615 ) ;
#60639=VECTOR ( 'NONE', #89199, 1000.000000000000000 ) ;
#60640=VECTOR ( 'NONE', #107296, 999.9999999999998863 ) ;
#60641=LINE ( 'NONE', #93925, #137212 ) ;
#60642=DIRECTION ( 'NONE',  ( -0.7071067811865487940, 0.7071067811865463515, -0.000000000000000000 ) ) ;
#60644=CARTESIAN_POINT ( 'NONE',  ( -1.499999999999989120, 16.77039438581778796, 0.4657186855307757778 ) ) ;
#60645=CARTESIAN_POINT ( 'NONE',  ( 6.799968779831584875, 8.259292476615627265, 16.85664084051839495 ) ) ;
#60646=VECTOR ( 'NONE', #122718, 999.9999999999998863 ) ;
#60647=EDGE_LOOP ( 'NONE', ( #105658, #43759, #93233, #142205 ) ) ;
#60648=DIRECTION ( 'NONE',  ( -0.7071067811865487940, 0.7071067811865463515, -0.000000000000000000 ) ) ;
#60650=EDGE_CURVE ( 'NONE', #112059, #98928, #117480, .T. ) ;
#60651=DIRECTION ( 'NONE',  ( -0.000000000000000000, -0.3543493200069152693, 0.9351131265310292928 ) ) ;
#60652=LINE ( 'NONE', #117108, #46039 ) ;
#60654=VERTEX_POINT ( 'NONE', #96431 ) ;
#60655=EDGE_LOOP ( 'NONE', ( #35435, #40685, #61628, #30497 ) ) ;
#60656=ORIENTED_EDGE ( 'NONE', *, *, #74756, .F. ) ;
#60657=CARTESIAN_POINT ( 'NONE',  ( 60.29974487139158867, -27.71228299555248142, 4.000000000000000000 ) ) ;
#60658=DIRECTION ( 'NONE',  ( 0.7071067811865487940, 0.7071067811865463515, 0.000000000000000000 ) ) ;
#60660=CARTESIAN_POINT ( 'NONE',  ( -0.4892135623730947680, -27.52281430457055578, 5.000000000000000000 ) ) ;
#60664=EDGE_CURVE ( 'NONE', #63809, #31526, #9418, .T. ) ;
#60665=VECTOR ( 'NONE', #64298, 1000.000000000000000 ) ;
#60667=VECTOR ( 'NONE', #74998, 1000.000000000000000 ) ;
#60668=LINE ( 'NONE', #93954, #32184 ) ;
#60669=EDGE_CURVE ( 'NONE', #95099, #41659, #64557, .T. ) ;
#60671=LINE ( 'NONE', #104831, #136964 ) ;
#60672=VECTOR ( 'NONE', #32604, 1000.000000000000000 ) ;
#60673=LINE ( 'NONE', #14956, #85855 ) ;
#60674=ORIENTED_EDGE ( 'NONE', *, *, #58095, .T. ) ;
#60675=DIRECTION ( 'NONE',  ( -0.7071067811865487940, 0.7071067811865463515, -0.000000000000000000 ) ) ;
#60676=VECTOR ( 'NONE', #140351, 1000.000000000000000 ) ;
#60677=ORIENTED_EDGE ( 'NONE', *, *, #110587, .F. ) ;
#60678=CARTESIAN_POINT ( 'NONE',  ( -6.299744871391586898, -27.71228299555210484, 4.000000000000000000 ) ) ;
#60680=ORIENTED_EDGE ( 'NONE', *, *, #10444, .T. ) ;
#60682=DIRECTION ( 'NONE',  ( -0.6830127018922181881, 0.6830127018922202975, -0.2588190451025214056 ) ) ;
#60683=ORIENTED_EDGE ( 'NONE', *, *, #124157, .F. ) ;
#60684=LINE ( 'NONE', #85055, #101701 ) ;
#60685=VERTEX_POINT ( 'NONE', #105887 ) ;
#60686=CARTESIAN_POINT ( 'NONE',  ( -6.792893218813405909, -11.24070752338416845, 5.000000000000000000 ) ) ;
#60687=ORIENTED_EDGE ( 'NONE', *, *, #126316, .F. ) ;
#60689=LINE ( 'NONE', #80276, #137604 ) ;
#60692=DIRECTION ( 'NONE',  ( 0.6830127018922180770, -0.6830127018922204085, -0.2588190451025213501 ) ) ;
#60693=ORIENTED_EDGE ( 'NONE', *, *, #95661, .F. ) ;
#60695=CARTESIAN_POINT ( 'NONE',  ( -3.299744871391591339, -27.71228299555208352, 4.000000000000000000 ) ) ;
#60697=VECTOR ( 'NONE', #56462, 1000.000000000000000 ) ;
#60699=DIRECTION ( 'NONE',  ( 0.6830127018922181881, 0.6830127018922202975, -0.2588190451025214056 ) ) ;
#60701=ORIENTED_EDGE ( 'NONE', *, *, #108086, .F. ) ;
#60702=PLANE ( 'NONE',  #67670 ) ;
#60703=ORIENTED_EDGE ( 'NONE', *, *, #67098, .T. ) ;
#60705=FACE_OUTER_BOUND ( 'NONE', #125317, .T. ) ;
#60706=CARTESIAN_POINT ( 'NONE',  ( -60.48921356237309510, -27.52281430457097500, 5.000000000000000000 ) ) ;
#60707=AXIS2_PLACEMENT_3D ( 'NONE', #49580, #28523, #59732 ) ;
#60708=DIRECTION ( 'NONE',  ( -0.000000000000000000, 0.000000000000000000, 1.000000000000000000 ) ) ;
#60710=DIRECTION ( 'NONE',  ( -0.6830127018922181881, 0.6830127018922202975, -0.2588190451025214056 ) ) ;
#60711=CARTESIAN_POINT ( 'NONE',  ( 36.18398860626899705, 28.73617430169812437, 5.000000000000000000 ) ) ;
#60713=DIRECTION ( 'NONE',  ( -0.6830127018922180770, -0.6830127018922204085, -0.2588190451025213501 ) ) ;
#60714=FACE_OUTER_BOUND ( 'NONE', #63383, .T. ) ;
#60715=ORIENTED_EDGE ( 'NONE', *, *, #72986, .T. ) ;
#60716=LINE ( 'NONE', #17170, #124791 ) ;
#60718=EDGE_LOOP ( 'NONE', ( #10883, #83384, #110967, #5556 ) ) ;
#60719=ORIENTED_EDGE ( 'NONE', *, *, #87769, .T. ) ;
#60720=VERTEX_POINT ( 'NONE', #72631 ) ;
#60721=ADVANCED_FACE ( 'NONE', ( #84204 ), #127689, .T. ) ;
#60723=VERTEX_POINT ( 'NONE', #6551 ) ;
#60724=EDGE_CURVE ( 'NONE', #49304, #31707, #94321, .T. ) ;
#60725=FACE_OUTER_BOUND ( 'NONE', #137226, .T. ) ;
#60726=CARTESIAN_POINT ( 'NONE',  ( 8.816011393731004731, 28.73617430169781173, 5.000000000000000000 ) ) ;
#60727=EDGE_CURVE ( 'NONE', #53759, #96641, #95021, .T. ) ;
#60729=CARTESIAN_POINT ( 'NONE',  ( -23.99999999999982592, -3.412538124160721331, 4.000000000000000000 ) ) ;
#60731=VECTOR ( 'NONE', #26397, 1000.000000000000000 ) ;
#60733=AXIS2_PLACEMENT_3D ( 'NONE', #3599, #124000, #45051 ) ;
#60735=DIRECTION ( 'NONE',  ( -0.7071067811865486830, -0.7071067811865464625, 0.000000000000000000 ) ) ;
#60736=FACE_OUTER_BOUND ( 'NONE', #39971, .T. ) ;
#60737=VECTOR ( 'NONE', #142255, 1000.000000000000000 ) ;
#60739=VERTEX_POINT ( 'NONE', #39988 ) ;
#60740=EDGE_CURVE ( 'NONE', #128218, #132831, #116790, .T. ) ;
#60741=CARTESIAN_POINT ( 'NONE',  ( -6.183988606268994381, 28.73617430169791476, 5.000000000000000000 ) ) ;
#60742=AXIS2_PLACEMENT_3D ( 'NONE', #140192, #40879, #72113 ) ;
#60743=PLANE ( 'NONE',  #87220 ) ;
#60744=DIRECTION ( 'NONE',  ( 1.000000000000000000, 0.000000000000000000, 0.000000000000000000 ) ) ;
#60745=VECTOR ( 'NONE', #24961, 1000.000000000000000 ) ;
#60747=EDGE_LOOP ( 'NONE', ( #80350, #25038, #46910, #92751 ) ) ;
#60748=ORIENTED_EDGE ( 'NONE', *, *, #54209, .F. ) ;
#60751=EDGE_CURVE ( 'NONE', #21250, #33900, #8010, .T. ) ;
#60752=CARTESIAN_POINT ( 'NONE',  ( 31.40832548098981647, -0.7407075233842735917, 14.76736230305387920 ) ) ;
#60753=DIRECTION ( 'NONE',  ( 0.7071067811865486830, -0.7071067811865464625, -0.000000000000000000 ) ) ;
#60756=ADVANCED_FACE ( 'NONE', ( #17473 ), #128400, .F. ) ;
#60757=CARTESIAN_POINT ( 'NONE',  ( 36.18398860626899705, 28.73617430169812437, 5.000000000000000000 ) ) ;
#60758=VERTEX_POINT ( 'NONE', #42116 ) ;
#60759=VERTEX_POINT ( 'NONE', #119619 ) ;
#60760=ORIENTED_EDGE ( 'NONE', *, *, #2288, .T. ) ;
#60761=ORIENTED_EDGE ( 'NONE', *, *, #34335, .T. ) ;
#60762=AXIS2_PLACEMENT_3D ( 'NONE', #71107, #2954, #81268 ) ;
#60763=LINE ( 'NONE', #49861, #29333 ) ;
#60764=AXIS2_PLACEMENT_3D ( 'NONE', #20384, #76224, #142901 ) ;
#60765=DIRECTION ( 'NONE',  ( 0.7071067811865487940, -0.7071067811865463515, 0.000000000000000000 ) ) ;
#60766=VERTEX_POINT ( 'NONE', #63168 ) ;
#60767=CARTESIAN_POINT ( 'NONE',  ( 31.82816939922330945, 0.7592924766157138627, 4.000000000000000000 ) ) ;
#60768=LINE ( 'NONE', #94050, #128167 ) ;
#60769=VECTOR ( 'NONE', #35304, 1000.000000000000000 ) ;
#60770=PLANE ( 'NONE',  #87393 ) ;
#60771=ADVANCED_FACE ( 'NONE', ( #86328 ), #130547, .T. ) ;
#60772=CARTESIAN_POINT ( 'NONE',  ( -42.18398860626899705, 28.73617430169816700, 5.000000000000000000 ) ) ;
#60773=VECTOR ( 'NONE', #36943, 1000.000000000000000 ) ;
#60774=LINE ( 'NONE', #60026, #83834 ) ;
#60775=ORIENTED_EDGE ( 'NONE', *, *, #31453, .T. ) ;
#60776=CARTESIAN_POINT ( 'NONE',  ( 20.99999999999985079, 8.816494571476654940, 4.604407763760433703 ) ) ;
#60778=ORIENTED_EDGE ( 'NONE', *, *, #72475, .F. ) ;
#60779=DIRECTION ( 'NONE',  ( -0.7071067811865486830, 0.7071067811865464625, 0.000000000000000000 ) ) ;
#60780=VERTEX_POINT ( 'NONE', #140674 ) ;
#60782=LINE ( 'NONE', #61487, #124569 ) ;
#60783=ORIENTED_EDGE ( 'NONE', *, *, #71256, .T. ) ;
#60784=ORIENTED_EDGE ( 'NONE', *, *, #3817, .T. ) ;
#60786=VECTOR ( 'NONE', #106701, 1000.000000000000000 ) ;
#60787=VERTEX_POINT ( 'NONE', #41364 ) ;
#60790=CARTESIAN_POINT ( 'NONE',  ( -39.48921356237310221, -27.52281430457082934, 5.000000000000000000 ) ) ;
#60791=EDGE_CURVE ( 'NONE', #106916, #64860, #129808, .T. ) ;
#60792=AXIS2_PLACEMENT_3D ( 'NONE', #59818, #5392, #49674 ) ;
#60793=LINE ( 'NONE', #41130, #66137 ) ;
#60794=VECTOR ( 'NONE', #39804, 1000.000000000000227 ) ;
#60795=CARTESIAN_POINT ( 'NONE',  ( -39.18398860626899705, 28.73617430169814568, 5.000000000000000000 ) ) ;
#60798=VERTEX_POINT ( 'NONE', #34800 ) ;
#60800=EDGE_CURVE ( 'NONE', #19214, #105592, #13334, .T. ) ;
#60802=ORIENTED_EDGE ( 'NONE', *, *, #89071, .T. ) ;
#60803=VECTOR ( 'NONE', #21744, 1000.000000000000227 ) ;
#60806=ORIENTED_EDGE ( 'NONE', *, *, #83262, .T. ) ;
#60807=CARTESIAN_POINT ( 'NONE',  ( 32.99451991528749062, 28.92564299267960948, 4.000000000000000000 ) ) ;
#60808=DIRECTION ( 'NONE',  ( -0.7071067811865486830, -0.7071067811865464625, 0.000000000000000000 ) ) ;
#60809=ADVANCED_FACE ( 'NONE', ( #53703 ), #142836, .F. ) ;
#60810=DIRECTION ( 'NONE',  ( -0.6830127018922181881, 0.6830127018922202975, -0.2588190451025214056 ) ) ;
#60811=CARTESIAN_POINT ( 'NONE',  ( 15.48921356237309510, -27.52281430457066236, 5.000000000000000000 ) ) ;
#60812=ORIENTED_EDGE ( 'NONE', *, *, #99781, .T. ) ;
#60813=CARTESIAN_POINT ( 'NONE',  ( -69.48921356237309510, -27.52281430457103895, 5.000000000000000000 ) ) ;
#60814=VECTOR ( 'NONE', #100242, 1000.000000000000000 ) ;
#60815=ORIENTED_EDGE ( 'NONE', *, *, #67100, .T. ) ;
#60816=( BOUNDED_CURVE ( )  B_SPLINE_CURVE ( 3, ( #84126, #41287, #72558, #51477 ),
 .UNSPECIFIED., .F., .F. ) 
 B_SPLINE_CURVE_WITH_KNOTS ( ( 4, 4 ),
 ( 4.350170835173031492, 4.500739107949213391 ),
 .UNSPECIFIED. ) 
 CURVE ( )  GEOMETRIC_REPRESENTATION_ITEM ( )  RATIONAL_B_SPLINE_CURVE ( ( 1.000000000000000000, 0.9981116584018958626, 0.9981116584018958626, 1.000000000000000000 ) ) 
 REPRESENTATION_ITEM ( '' )  );
#60818=CARTESIAN_POINT ( 'NONE',  ( 17.99451991528748351, 28.92564299267950645, 4.000000000000000000 ) ) ;
#60819=LINE ( 'NONE', #138339, #99167 ) ;
#60820=CARTESIAN_POINT ( 'NONE',  ( 27.18398860626900060, 28.73617430169806042, 5.000000000000000000 ) ) ;
#60821=VERTEX_POINT ( 'NONE', #89176 ) ;
#60822=VERTEX_POINT ( 'NONE', #99298 ) ;
#60823=ORIENTED_EDGE ( 'NONE', *, *, #51814, .T. ) ;
#60824=DIRECTION ( 'NONE',  ( 0.6830127018922180770, -0.6830127018922204085, -0.2588190451025213501 ) ) ;
#60825=DIRECTION ( 'NONE',  ( 0.7071067811865486830, -0.7071067811865464625, -0.000000000000000000 ) ) ;
#60826=VECTOR ( 'NONE', #97706, 1000.000000000000227 ) ;
#60829=AXIS2_PLACEMENT_3D ( 'NONE', #79302, #35787, #56832 ) ;
#60830=PLANE ( 'NONE',  #57859 ) ;
#60831=ADVANCED_FACE ( 'NONE', ( #110883 ), #100054, .F. ) ;
#60832=VECTOR ( 'NONE', #127251, 1000.000000000000000 ) ;
#60833=DIRECTION ( 'NONE',  ( -0.000000000000000000, 0.000000000000000000, 1.000000000000000000 ) ) ;
#60834=AXIS2_PLACEMENT_3D ( 'NONE', #100678, #23826, #44914 ) ;
#60835=LINE ( 'NONE', #28879, #53177 ) ;
#60836=ADVANCED_FACE ( 'NONE', ( #42828 ), #33401, .F. ) ;
#60837=DIRECTION ( 'NONE',  ( -0.3543493200069162685, -0.000000000000000000, -0.9351131265310288487 ) ) ;
#60838=FACE_OUTER_BOUND ( 'NONE', #9800, .T. ) ;
#60839=VERTEX_POINT ( 'NONE', #23923 ) ;
#60841=VECTOR ( 'NONE', #77102, 1000.000000000000000 ) ;
#60843=DIRECTION ( 'NONE',  ( 0.7071067811865486830, -0.7071067811865464625, -0.000000000000000000 ) ) ;
#60844=ORIENTED_EDGE ( 'NONE', *, *, #12062, .F. ) ;
#60845=LINE ( 'NONE', #1557, #22724 ) ;
#60846=EDGE_CURVE ( 'NONE', #27137, #107846, #77602, .T. ) ;
#60848=ORIENTED_EDGE ( 'NONE', *, *, #101005, .F. ) ;
#60849=EDGE_CURVE ( 'NONE', #93195, #80263, #88470, .T. ) ;
#60851=DIRECTION ( 'NONE',  ( -0.3543493200069162685, -0.000000000000000000, -0.9351131265310288487 ) ) ;
#60852=ORIENTED_EDGE ( 'NONE', *, *, #102377, .F. ) ;
#60853=PLANE ( 'NONE',  #16474 ) ;
#60855=LINE ( 'NONE', #114458, #21995 ) ;
#60856=CARTESIAN_POINT ( 'NONE',  ( 0.000000000000000000, 0.000000000000000000, 5.000000000000000000 ) ) ;
#60858=CARTESIAN_POINT ( 'NONE',  ( 0.4892135623730947680, -27.52281430457055578, 5.000000000000000000 ) ) ;
#60859=VECTOR ( 'NONE', #80091, 1000.000000000000000 ) ;
#60860=DIRECTION ( 'NONE',  ( -0.7071067811865487940, 0.7071067811865463515, -0.000000000000000000 ) ) ;
#60861=CARTESIAN_POINT ( 'NONE',  ( 24.48921356237309510, -27.52281430457072631, 5.000000000000000000 ) ) ;
#60863=CARTESIAN_POINT ( 'NONE',  ( 54.48921356237310221, -27.52281430457093236, 5.000000000000000000 ) ) ;
#60866=CARTESIAN_POINT ( 'NONE',  ( -62.99451991528749772, 28.92564299267982264, 4.000000000000000000 ) ) ;
#60867=CARTESIAN_POINT ( 'NONE',  ( 11.99999999999991296, -8.731860332648832212, -2.120594902707510165 ) ) ;
#60868=DIRECTION ( 'NONE',  ( 0.3543493200069162685, -0.000000000000000000, -0.9351131265310288487 ) ) ;
#60869=ORIENTED_EDGE ( 'NONE', *, *, #887, .T. ) ;
#60870=EDGE_CURVE ( 'NONE', #60255, #133359, #112437, .T. ) ;
#60871=VECTOR ( 'NONE', #39912, 999.9999999999998863 ) ;
#60872=EDGE_LOOP ( 'NONE', ( #239, #117484, #38157, #51803 ) ) ;
#60875=ORIENTED_EDGE ( 'NONE', *, *, #72299, .T. ) ;
#60876=ORIENTED_EDGE ( 'NONE', *, *, #59902, .T. ) ;
#60878=VECTOR ( 'NONE', #114539, 1000.000000000000227 ) ;
#60879=CARTESIAN_POINT ( 'NONE',  ( 11.28769006033964928, -21.73547319004781642, 4.999917730833663754 ) ) ;
#60883=ORIENTED_EDGE ( 'NONE', *, *, #103611, .F. ) ;
#60884=DIRECTION ( 'NONE',  ( 0.3543493200069163240, 0.000000000000000000, 0.9351131265310288487 ) ) ;
#60886=CARTESIAN_POINT ( 'NONE',  ( -39.18398860626899705, 28.73617430169814568, 5.000000000000000000 ) ) ;
#60889=CARTESIAN_POINT ( 'NONE',  ( -53.99451991528749062, 28.92564299267975869, 4.000000000000000000 ) ) ;
#60891=CARTESIAN_POINT ( 'NONE',  ( 6.489213562373093325, -27.52281430457059841, 5.000000000000000000 ) ) ;
#60892=CARTESIAN_POINT ( 'NONE',  ( 54.18398860626899705, 28.73617430169825226, 5.000000000000000000 ) ) ;
#60893=DIRECTION ( 'NONE',  ( 0.6830127018922180770, -0.6830127018922204085, -0.2588190451025213501 ) ) ;
#60897=EDGE_CURVE ( 'NONE', #95607, #10314, #66707, .T. ) ;
#60899=ORIENTED_EDGE ( 'NONE', *, *, #125319, .F. ) ;
#60901=VECTOR ( 'NONE', #16844, 1000.000000000000114 ) ;
#60902=AXIS2_PLACEMENT_3D ( 'NONE', #131627, #132368, #54098 ) ;
#60903=DIRECTION ( 'NONE',  ( -0.7071067811865486830, -0.7071067811865464625, 0.000000000000000000 ) ) ;
#60904=ORIENTED_EDGE ( 'NONE', *, *, #118026, .T. ) ;
#60906=ADVANCED_FACE ( 'NONE', ( #22449 ), #133403, .T. ) ;
#60910=ORIENTED_EDGE ( 'NONE', *, *, #7495, .T. ) ;
#60911=LINE ( 'NONE', #41977, #21188 ) ;
#60912=ORIENTED_EDGE ( 'NONE', *, *, #22315, .F. ) ;
#60913=FACE_OUTER_BOUND ( 'NONE', #86849, .T. ) ;
#60914=AXIS2_PLACEMENT_3D ( 'NONE', #143250, #75863, #42542 ) ;
#60915=CARTESIAN_POINT ( 'NONE',  ( 39.48921356237310221, -27.52281430457082934, 5.000000000000000000 ) ) ;
#60916=CARTESIAN_POINT ( 'NONE',  ( 24.59263130292903554, 0.9595543924999635488, 5.000000000000000000 ) ) ;
#60917=LINE ( 'NONE', #50009, #36988 ) ;
#60918=ORIENTED_EDGE ( 'NONE', *, *, #84010, .T. ) ;
#60920=EDGE_CURVE ( 'NONE', #69887, #123337, #110183, .T. ) ;
#60921=ORIENTED_EDGE ( 'NONE', *, *, #97145, .F. ) ;
#60922=LINE ( 'NONE', #105770, #5067 ) ;
#60923=EDGE_CURVE ( 'NONE', #16634, #127668, #36229, .T. ) ;
#60924=CARTESIAN_POINT ( 'NONE',  ( -30.70710678118632941, -3.740707523384243505, 5.000000000000000000 ) ) ;
#60926=VECTOR ( 'NONE', #47700, 1000.000000000000227 ) ;
#60927=DIRECTION ( 'NONE',  ( 1.000000000000000000, 0.000000000000000000, 0.000000000000000000 ) ) ;
#60928=EDGE_CURVE ( 'NONE', #103350, #35337, #82575, .T. ) ;
#60929=LINE ( 'NONE', #5023, #100957 ) ;
#60930=VERTEX_POINT ( 'NONE', #49261 ) ;
#60931=ORIENTED_EDGE ( 'NONE', *, *, #22429, .T. ) ;
#60933=EDGE_LOOP ( 'NONE', ( #39870, #127876, #30655, #50457 ) ) ;
#60934=VERTEX_POINT ( 'NONE', #126768 ) ;
#60937=VECTOR ( 'NONE', #26196, 1000.000000000000000 ) ;
#60939=VECTOR ( 'NONE', #69875, 1000.000000000000000 ) ;
#60940=DIRECTION ( 'NONE',  ( -0.7071067811865487940, 0.7071067811865463515, 0.000000000000000000 ) ) ;
#60941=CARTESIAN_POINT ( 'NONE',  ( -23.29387692260788612, 22.22500000000000142, 4.000000000000000000 ) ) ;
#60942=VERTEX_POINT ( 'NONE', #26758 ) ;
#60943=PLANE ( 'NONE',  #36794 ) ;
#60944=AXIS2_PLACEMENT_3D ( 'NONE', #81470, #26351, #90910 ) ;
#60945=CARTESIAN_POINT ( 'NONE',  ( -24.81246187583929697, -22.22500000000000142, 4.000000000000000000 ) ) ;
#60946=EDGE_CURVE ( 'NONE', #92779, #50212, #102199, .T. ) ;
#60947=VECTOR ( 'NONE', #133248, 1000.000000000000000 ) ;
#60950=DIRECTION ( 'NONE',  ( -0.7071067811865486830, 0.7071067811865464625, 0.000000000000000000 ) ) ;
#60952=DIRECTION ( 'NONE',  ( 0.7071067811865487940, 0.7071067811865463515, 0.000000000000000000 ) ) ;
#60953=FACE_BOUND ( 'NONE', #121919, .T. ) ;
#60954=ORIENTED_EDGE ( 'NONE', *, *, #116864, .F. ) ;
#60955=DIRECTION ( 'NONE',  ( 0.7071067811865486830, -0.7071067811865464625, -0.000000000000000000 ) ) ;
#60956=DIRECTION ( 'NONE',  ( 0.7071067811865487940, 0.7071067811865463515, -0.000000000000000000 ) ) ;
#60957=VERTEX_POINT ( 'NONE', #69588 ) ;
#60958=EDGE_CURVE ( 'NONE', #35148, #61512, #115157, .T. ) ;
#60959=LINE ( 'NONE', #105118, #34236 ) ;
#60960=ORIENTED_EDGE ( 'NONE', *, *, #139279, .F. ) ;
#60961=ORIENTED_EDGE ( 'NONE', *, *, #113419, .F. ) ;
#60965=EDGE_LOOP ( 'NONE', ( #40020, #30887, #78728, #22700 ) ) ;
#60966=FACE_OUTER_BOUND ( 'NONE', #24748, .T. ) ;
#60967=LINE ( 'NONE', #107258, #143379 ) ;
#60969=LINE ( 'NONE', #130474, #52866 ) ;
#60970=CARTESIAN_POINT ( 'NONE',  ( -2.999999999999969802, -0.4125381241607498639, 4.000000000000000000 ) ) ;
#60971=VECTOR ( 'NONE', #122419, 1000.000000000000000 ) ;
#60974=DIRECTION ( 'NONE',  ( 0.6830127018922181881, 0.6830127018922202975, -0.2588190451025214056 ) ) ;
#60975=FACE_OUTER_BOUND ( 'NONE', #85553, .T. ) ;
#60977=CARTESIAN_POINT ( 'NONE',  ( -21.70710678118638270, -6.740707523384218192, 5.000000000000000000 ) ) ;
#60978=EDGE_CURVE ( 'NONE', #667, #79834, #48516, .T. ) ;
#60979=ORIENTED_EDGE ( 'NONE', *, *, #41209, .T. ) ;
#60980=ORIENTED_EDGE ( 'NONE', *, *, #143326, .F. ) ;
#60982=EDGE_LOOP ( 'NONE', ( #29036, #117426, #11481 ) ) ;
#60983=ORIENTED_EDGE ( 'NONE', *, *, #80195, .F. ) ;
#60984=AXIS2_PLACEMENT_3D ( 'NONE', #87687, #101232, #14228 ) ;
#60985=ORIENTED_EDGE ( 'NONE', *, *, #65994, .T. ) ;
#60987=ADVANCED_FACE ( 'NONE', ( #35542 ), #68870, .F. ) ;
#60988=CARTESIAN_POINT ( 'NONE',  ( -11.99999999999992006, -3.485240976185087991, -4.108735105802425736 ) ) ;
#60989=ORIENTED_EDGE ( 'NONE', *, *, #64980, .F. ) ;
#60991=ORIENTED_EDGE ( 'NONE', *, *, #882, .F. ) ;
#60992=DIRECTION ( 'NONE',  ( -0.000000000000000000, 0.3543493200069153248, 0.9351131265310292928 ) ) ;
#60993=VECTOR ( 'NONE', #68850, 1000.000000000000000 ) ;
#60995=VECTOR ( 'NONE', #124970, 1000.000000000000000 ) ;
#60997=ORIENTED_EDGE ( 'NONE', *, *, #28065, .T. ) ;
#60999=DIRECTION ( 'NONE',  ( -0.7071067811865486830, -0.7071067811865464625, 0.000000000000000000 ) ) ;
#61000=CARTESIAN_POINT ( 'NONE',  ( 15.70701326429294475, -21.74070752338405654, 4.999753212805220670 ) ) ;
#61001=CARTESIAN_POINT ( 'NONE',  ( -11.81601139373100651, 28.73617430169779041, 5.000000000000000000 ) ) ;
#61002=ORIENTED_EDGE ( 'NONE', *, *, #130615, .F. ) ;
#61004=PLANE ( 'NONE',  #86618 ) ;
#61005=ORIENTED_EDGE ( 'NONE', *, *, #20708, .F. ) ;
#61006=FACE_OUTER_BOUND ( 'NONE', #58484, .T. ) ;
#61008=DIRECTION ( 'NONE',  ( -0.6830127018922181881, 0.6830127018922202975, -0.2588190451025214056 ) ) ;
#61010=LINE ( 'NONE', #2253, #23844 ) ;
#61012=EDGE_LOOP ( 'NONE', ( #115933, #42082, #128542, #80411, #131649 ) ) ;
#61013=CARTESIAN_POINT ( 'NONE',  ( -21.48921356237309155, -27.52281430457070499, 5.000000000000000000 ) ) ;
#61014=ADVANCED_FACE ( 'NONE', ( #113771 ), #102908, .F. ) ;
#61015=DIRECTION ( 'NONE',  ( 0.7071067811865487940, 0.7071067811865463515, -0.000000000000000000 ) ) ;
#61016=LINE ( 'NONE', #71145, #134785 ) ;
#61017=VERTEX_POINT ( 'NONE', #70321 ) ;
#61018=LINE ( 'NONE', #103722, #53633 ) ;
#61019=VECTOR ( 'NONE', #82298, 1000.000000000000000 ) ;
#61022=ADVANCED_FACE ( 'NONE', ( #47847 ), #4221, .F. ) ;
#61023=DIRECTION ( 'NONE',  ( -0.000000000000000000, 0.3543493200069153248, 0.9351131265310292928 ) ) ;
#61024=ORIENTED_EDGE ( 'NONE', *, *, #30675, .T. ) ;
#61025=EDGE_CURVE ( 'NONE', #32778, #91632, #37662, .T. ) ;
#61026=VERTEX_POINT ( 'NONE', #2855 ) ;
#61027=VECTOR ( 'NONE', #32337, 1000.000000000000227 ) ;
#61029=CARTESIAN_POINT ( 'NONE',  ( -45.18398860626900415, 28.73617430169818832, 5.000000000000000000 ) ) ;
#61030=ORIENTED_EDGE ( 'NONE', *, *, #92127, .F. ) ;
#61031=DIRECTION ( 'NONE',  ( 0.7071067811865487940, 0.7071067811865463515, -0.000000000000000000 ) ) ;
#61032=CARTESIAN_POINT ( 'NONE',  ( 12.79289321881336683, 15.75929247661555976, 5.000000000000000000 ) ) ;
#61034=ORIENTED_EDGE ( 'NONE', *, *, #117774, .F. ) ;
#61036=DIRECTION ( 'NONE',  ( 1.000000000000000000, 0.000000000000000000, 0.000000000000000000 ) ) ;
#61037=CARTESIAN_POINT ( 'NONE',  ( -51.29974487139158867, -27.71228299555242103, 4.000000000000000000 ) ) ;
#61038=DIRECTION ( 'NONE',  ( -0.7071067811865486830, -0.7071067811865464625, 0.000000000000000000 ) ) ;
#61039=CARTESIAN_POINT ( 'NONE',  ( 24.81349135397623584, -15.74070752338412049, 8.904080028138885439 ) ) ;
#61040=PLANE ( 'NONE',  #44822 ) ;
#61041=AXIS2_PLACEMENT_3D ( 'NONE', #78279, #31908, #110157 ) ;
#61042=LINE ( 'NONE', #116788, #21241 ) ;
#61043=DIRECTION ( 'NONE',  ( -0.000000000000000000, 0.3543493200069153248, 0.9351131265310292928 ) ) ;
#61047=ADVANCED_FACE ( 'NONE', ( #114469 ), #57286, .F. ) ;
#61048=VECTOR ( 'NONE', #137060, 1000.000000000000227 ) ;
#61049=ORIENTED_EDGE ( 'NONE', *, *, #20378, .F. ) ;
#61050=ORIENTED_EDGE ( 'NONE', *, *, #1862, .T. ) ;
#61052=VERTEX_POINT ( 'NONE', #92717 ) ;
#61053=VERTEX_POINT ( 'NONE', #136952 ) ;
#61054=ORIENTED_EDGE ( 'NONE', *, *, #37186, .T. ) ;
#61055=VECTOR ( 'NONE', #140729, 999.9999999999998863 ) ;
#61056=LINE ( 'NONE', #117490, #91913 ) ;
#61057=LINE ( 'NONE', #113798, #26884 ) ;
#61058=CARTESIAN_POINT ( 'NONE',  ( -34.92500000000001137, 22.22500000000000142, 4.000000000000000000 ) ) ;
#61059=ADVANCED_FACE ( 'NONE', ( #46422 ), #27450, .F. ) ;
#61062=FACE_OUTER_BOUND ( 'NONE', #7039, .T. ) ;
#61063=FACE_OUTER_BOUND ( 'NONE', #32872, .T. ) ;
#61064=CARTESIAN_POINT ( 'NONE',  ( -13.17183060077638324, 6.759292476615645917, 4.000000000000000000 ) ) ;
#61067=CARTESIAN_POINT ( 'NONE',  ( -30.41161490594810246, 22.22500000000000497, 4.777194822843814137 ) ) ;
#61068=DIRECTION ( 'NONE',  ( -0.000000000000000000, 0.3543493200069152138, -0.9351131265310292928 ) ) ;
#61069=DIRECTION ( 'NONE',  ( 0.7071067811865487940, 0.7071067811865463515, 0.000000000000000000 ) ) ;
#61070=VECTOR ( 'NONE', #25961, 999.9999999999998863 ) ;
#61071=DIRECTION ( 'NONE',  ( 0.6830127018922180770, -0.6830127018922204085, -0.2588190451025213501 ) ) ;
#61072=CARTESIAN_POINT ( 'NONE',  ( 3.792893218813431222, -5.240707523384228850, 5.000000000000000000 ) ) ;
#61074=LINE ( 'NONE', #113969, #28244 ) ;
#61075=AXIS2_PLACEMENT_3D ( 'NONE', #127495, #28903, #73142 ) ;
#61077=ORIENTED_EDGE ( 'NONE', *, *, #79714, .T. ) ;
#61078=ORIENTED_EDGE ( 'NONE', *, *, #132909, .F. ) ;
#61080=ORIENTED_EDGE ( 'NONE', *, *, #57618, .T. ) ;
#61081=CARTESIAN_POINT ( 'NONE',  ( 48.48921356237309510, -27.52281430457089328, 5.000000000000000000 ) ) ;
#61082=EDGE_CURVE ( 'NONE', #32915, #48791, #134847, .T. ) ;
#61083=LINE ( 'NONE', #105242, #13136 ) ;
#61084=ORIENTED_EDGE ( 'NONE', *, *, #104030, .T. ) ;
#61085=LINE ( 'NONE', #83514, #13202 ) ;
#61087=EDGE_CURVE ( 'NONE', #93683, #35648, #105028, .T. ) ;
#61089=DIRECTION ( 'NONE',  ( 0.7071067811865487940, 0.7071067811865463515, 0.000000000000000000 ) ) ;
#61090=LINE ( 'NONE', #16814, #104346 ) ;
#61092=VECTOR ( 'NONE', #111198, 1000.000000000000000 ) ;
#61093=ORIENTED_EDGE ( 'NONE', *, *, #112417, .F. ) ;
#61095=CARTESIAN_POINT ( 'NONE',  ( -57.18398860626899705, 28.73617430169827358, 5.000000000000000000 ) ) ;
#61097=DIRECTION ( 'NONE',  ( -0.7071067811865486830, -0.7071067811865464625, 0.000000000000000000 ) ) ;
#61098=ADVANCED_FACE ( 'NONE', ( #118009 ), #117313, .F. ) ;
#61099=CARTESIAN_POINT ( 'NONE',  ( 5.292893218813421896, 8.259292476615636147, 5.000000000000000000 ) ) ;
#61101=AXIS2_PLACEMENT_3D ( 'NONE', #127099, #105350, #84359 ) ;
#61103=VERTEX_POINT ( 'NONE', #29597 ) ;
#61105=ADVANCED_FACE ( 'NONE', ( #96967 ), #116624, .F. ) ;
#61106=ORIENTED_EDGE ( 'NONE', *, *, #34237, .F. ) ;
#61107=DIRECTION ( 'NONE',  ( 0.7071067811865487940, 0.7071067811865463515, 0.000000000000000000 ) ) ;
#61108=ADVANCED_FACE ( 'NONE', ( #141218 ), #74567, .F. ) ;
#61109=CARTESIAN_POINT ( 'NONE',  ( -13.49999999999990230, 16.77039438581778086, 0.4657186855308035334 ) ) ;
#61110=CARTESIAN_POINT ( 'NONE',  ( -38.99451991528749062, 28.92564299267965211, 4.000000000000000000 ) ) ;
#61111=PLANE ( 'NONE',  #30048 ) ;
#61112=VECTOR ( 'NONE', #134563, 1000.000000000000227 ) ;
#61113=ADVANCED_FACE ( 'NONE', ( #16578 ), #41935, .T. ) ;
#61115=EDGE_CURVE ( 'NONE', #38602, #78104, #39066, .T. ) ;
#61118=CARTESIAN_POINT ( 'NONE',  ( -6.792893218813405909, -14.24070752338413826, 5.000000000000000000 ) ) ;
#61119=DIRECTION ( 'NONE',  ( 0.7071067811865487940, -0.7071067811865463515, 0.000000000000000000 ) ) ;
#61120=ORIENTED_EDGE ( 'NONE', *, *, #126376, .F. ) ;
#61121=VERTEX_POINT ( 'NONE', #86147 ) ;
#61123=LINE ( 'NONE', #92972, #56249 ) ;
#61125=ORIENTED_EDGE ( 'NONE', *, *, #34479, .T. ) ;
#61126=CARTESIAN_POINT ( 'NONE',  ( -31.71896644758168904, 22.22500000000000142, 3.785114039161020738 ) ) ;
#61127=ORIENTED_EDGE ( 'NONE', *, *, #133868, .T. ) ;
#61129=ADVANCED_FACE ( 'NONE', ( #61568 ), #139840, .F. ) ;
#61131=FACE_BOUND ( 'NONE', #73208, .T. ) ;
#61132=DIRECTION ( 'NONE',  ( 0.000000000000000000, 1.000000000000000000, 0.000000000000000000 ) ) ;
#61134=ORIENTED_EDGE ( 'NONE', *, *, #62035, .F. ) ;
#61136=DIRECTION ( 'NONE',  ( 0.7071067811865486830, -0.7071067811865464625, -0.000000000000000000 ) ) ;
#61137=DIRECTION ( 'NONE',  ( -0.7071067811865486830, -0.7071067811865464625, -0.000000000000000000 ) ) ;
#61138=ORIENTED_EDGE ( 'NONE', *, *, #9409, .T. ) ;
#61139=VERTEX_POINT ( 'NONE', #28908 ) ;
#61140=CARTESIAN_POINT ( 'NONE',  ( 19.49999999999987210, -11.56887692260768929, 4.000000000000000000 ) ) ;
#61142=EDGE_CURVE ( 'NONE', #127177, #62908, #130373, .T. ) ;
#61145=VECTOR ( 'NONE', #27051, 1000.000000000000000 ) ;
#61147=CARTESIAN_POINT ( 'NONE',  ( 1.785015802758090020, -3.740707523384244837, 15.76143240460124773 ) ) ;
#61148=LINE ( 'NONE', #106698, #88950 ) ;
#61149=ORIENTED_EDGE ( 'NONE', *, *, #20518, .F. ) ;
#61150=CARTESIAN_POINT ( 'NONE',  ( 22.49999999999984723, -7.420205493532876950, -2.617629953481201088 ) ) ;
#61151=EDGE_CURVE ( 'NONE', #49472, #116795, #127502, .T. ) ;
#61152=VECTOR ( 'NONE', #95474, 1000.000000000000000 ) ;
#61153=CARTESIAN_POINT ( 'NONE',  ( 7.499999999999951150, -11.56887692260769107, 4.000000000000000000 ) ) ;
#61154=DIRECTION ( 'NONE',  ( 0.7071067811865487940, 0.7071067811865463515, 0.000000000000000000 ) ) ;
#61155=FACE_OUTER_BOUND ( 'NONE', #131350, .T. ) ;
#61156=CARTESIAN_POINT ( 'NONE',  ( -36.48921356237310221, -27.52281430457080802, 5.000000000000000000 ) ) ;
#61157=DIRECTION ( 'NONE',  ( -0.6830127018922180770, -0.6830127018922204085, -0.2588190451025213501 ) ) ;
#61158=VERTEX_POINT ( 'NONE', #73148 ) ;
#61161=CARTESIAN_POINT ( 'NONE',  ( 12.29974487139158512, -27.71228299555214747, 4.000000000000000000 ) ) ;
#61162=ORIENTED_EDGE ( 'NONE', *, *, #110888, .F. ) ;
#61163=ORIENTED_EDGE ( 'NONE', *, *, #75441, .F. ) ;
#61165=LINE ( 'NONE', #50243, #102247 ) ;
#61166=CARTESIAN_POINT ( 'NONE',  ( -34.92500000000001137, 4.512461875839451686, 4.000000000000000000 ) ) ;
#61167=ORIENTED_EDGE ( 'NONE', *, *, #65826, .T. ) ;
#61168=CARTESIAN_POINT ( 'NONE',  ( 32.99999999999977263, 4.552185695429122880, 5.000000000000000000 ) ) ;
#61170=CARTESIAN_POINT ( 'NONE',  ( -36.18398860626899705, 28.73617430169812437, 5.000000000000000000 ) ) ;
#61173=DIRECTION ( 'NONE',  ( 0.7071067811865487940, 0.7071067811865463515, 0.000000000000000000 ) ) ;
#61174=ORIENTED_EDGE ( 'NONE', *, *, #103674, .F. ) ;
#61175=LINE ( 'NONE', #74141, #102220 ) ;
#61176=EDGE_CURVE ( 'NONE', #137275, #33570, #56997, .T. ) ;
#61178=CARTESIAN_POINT ( 'NONE',  ( 37.04515773336643036, -21.74070752338406365, 21.72585301388593138 ) ) ;
#61180=FACE_OUTER_BOUND ( 'NONE', #129884, .T. ) ;
#61181=ORIENTED_EDGE ( 'NONE', *, *, #59209, .T. ) ;
#61183=FACE_OUTER_BOUND ( 'NONE', #36046, .T. ) ;
#61186=ORIENTED_EDGE ( 'NONE', *, *, #113742, .T. ) ;
#61187=VECTOR ( 'NONE', #112487, 999.9999999999998863 ) ;
#61188=DIRECTION ( 'NONE',  ( -0.3543493200069162685, -0.000000000000000000, -0.9351131265310288487 ) ) ;
#61190=FACE_OUTER_BOUND ( 'NONE', #68344, .T. ) ;
#61191=VERTEX_POINT ( 'NONE', #138380 ) ;
#61192=PLANE ( 'NONE',  #113369 ) ;
#61193=CARTESIAN_POINT ( 'NONE',  ( 13.49999999999990763, 9.431123077392092213, 4.000000000000000000 ) ) ;
#61194=CARTESIAN_POINT ( 'NONE',  ( -34.92500000000001137, -22.22500000000000142, 4.000000000000000000 ) ) ;
#61195=VECTOR ( 'NONE', #102363, 1000.000000000000114 ) ;
#61196=ADVANCED_FACE ( 'NONE', ( #17984 ), #50653, .F. ) ;
#61197=FACE_OUTER_BOUND ( 'NONE', #36389, .T. ) ;
#61199=EDGE_CURVE ( 'NONE', #90720, #9222, #40510, .T. ) ;
#61200=VERTEX_POINT ( 'NONE', #73835 ) ;
#61203=CARTESIAN_POINT ( 'NONE',  ( -6.489213562373093325, -27.52281430457059841, 5.000000000000000000 ) ) ;
#61204=VECTOR ( 'NONE', #124920, 1000.000000000000000 ) ;
#61205=EDGE_CURVE ( 'NONE', #83008, #33185, #99868, .T. ) ;
#61206=EDGE_CURVE ( 'NONE', #35333, #6025, #75284, .T. ) ;
#61208=DIRECTION ( 'NONE',  ( 0.6830127018922180770, -0.6830127018922204085, -0.2588190451025213501 ) ) ;
#61209=VECTOR ( 'NONE', #99610, 1000.000000000000000 ) ;
#61210=DIRECTION ( 'NONE',  ( -0.7071067811865487940, 0.7071067811865463515, 0.000000000000000000 ) ) ;
#61211=CARTESIAN_POINT ( 'NONE',  ( -8.293876922607989144, 22.22500000000000142, 4.000000000000000000 ) ) ;
#61212=LINE ( 'NONE', #48147, #60731 ) ;
#61214=EDGE_CURVE ( 'NONE', #99583, #85580, #99122, .T. ) ;
#61215=PLANE ( 'NONE',  #67382 ) ;
#61217=DIRECTION ( 'NONE',  ( -0.6830127018922181881, 0.6830127018922202975, -0.2588190451025214056 ) ) ;
#61218=DIRECTION ( 'NONE',  ( 0.6830127018922180770, -0.6830127018922204085, -0.2588190451025213501 ) ) ;
#61222=AXIS2_PLACEMENT_3D ( 'NONE', #51835, #32956, #96705 ) ;
#61223=ORIENTED_EDGE ( 'NONE', *, *, #30777, .T. ) ;
#61224=DIRECTION ( 'NONE',  ( -0.6830127018922180770, -0.6830127018922204085, -0.2588190451025213501 ) ) ;
#61225=VERTEX_POINT ( 'NONE', #76722 ) ;
#61226=ORIENTED_EDGE ( 'NONE', *, *, #70464, .T. ) ;
#61227=VECTOR ( 'NONE', #117269, 999.9999999999998863 ) ;
#61228=CARTESIAN_POINT ( 'NONE',  ( -17.01844734635659506, 18.75929247661552424, 20.33588619593446722 ) ) ;
#61229=EDGE_CURVE ( 'NONE', #21649, #3243, #142665, .T. ) ;
#61230=FACE_OUTER_BOUND ( 'NONE', #32725, .T. ) ;
#61231=FACE_OUTER_BOUND ( 'NONE', #69379, .T. ) ;
#61232=DIRECTION ( 'NONE',  ( 0.7071067811865487940, 0.7071067811865463515, 0.000000000000000000 ) ) ;
#61233=CARTESIAN_POINT ( 'NONE',  ( -11.20710678118646797, 9.759292476615620160, 5.000000000000000000 ) ) ;
#61234=PLANE ( 'NONE',  #112557 ) ;
#61235=EDGE_LOOP ( 'NONE', ( #48188, #48787, #34467, #14264 ) ) ;
#61236=CARTESIAN_POINT ( 'NONE',  ( 5.999999999999970690, -0.4125381241607533611, 4.000000000000000000 ) ) ;
#61239=DIRECTION ( 'NONE',  ( -0.7071067811865486830, 0.7071067811865464625, 0.000000000000000000 ) ) ;
#61240=DIRECTION ( 'NONE',  ( 0.7071067811865487940, -0.7071067811865463515, 0.000000000000000000 ) ) ;
#61241=CARTESIAN_POINT ( 'NONE',  ( 1.499999999999992673, 15.05218569542901186, 5.000000000000000000 ) ) ;
#61243=DIRECTION ( 'NONE',  ( -0.7071067811865486830, 0.7071067811865464625, 0.000000000000000000 ) ) ;
#61245=ORIENTED_EDGE ( 'NONE', *, *, #32180, .T. ) ;
#61247=LINE ( 'NONE', #119130, #104925 ) ;
#61248=CARTESIAN_POINT ( 'NONE',  ( -3.005480084712505828, 28.92564299267936079, 4.000000000000000000 ) ) ;
#61249=EDGE_CURVE ( 'NONE', #62473, #110860, #54262, .T. ) ;
#61250=VERTEX_POINT ( 'NONE', #120896 ) ;
#61251=AXIS2_PLACEMENT_3D ( 'NONE', #42923, #132804, #87122 ) ;
#61252=DIRECTION ( 'NONE',  ( 0.7071067811865486830, -0.7071067811865464625, -0.000000000000000000 ) ) ;
#61253=EDGE_CURVE ( 'NONE', #138628, #54912, #33915, .T. ) ;
#61254=ADVANCED_FACE ( 'NONE', ( #77440 ), #21601, .F. ) ;
#61257=EDGE_CURVE ( 'NONE', #45818, #130351, #132543, .T. ) ;
#61258=CARTESIAN_POINT ( 'NONE',  ( 34.47516574401890921, -10.50948238788426536, 4.998110765256835286 ) ) ;
#61259=VERTEX_POINT ( 'NONE', #122307 ) ;
#61260=VERTEX_POINT ( 'NONE', #44829 ) ;
#61262=ADVANCED_FACE ( 'NONE', ( #66540 ), #133238, .F. ) ;
#61263=LINE ( 'NONE', #126445, #3661 ) ;
#61264=PLANE ( 'NONE',  #55873 ) ;
#61266=EDGE_CURVE ( 'NONE', #132586, #142104, #86865, .T. ) ;
#61267=CARTESIAN_POINT ( 'NONE',  ( 29.99999999999979750, -13.44781430457068794, 5.000000000000000000 ) ) ;
#61269=ORIENTED_EDGE ( 'NONE', *, *, #84598, .T. ) ;
#61270=LINE ( 'NONE', #15523, #6665 ) ;
#61272=DIRECTION ( 'NONE',  ( -0.000000000000000000, 0.3543493200069153248, 0.9351131265310292928 ) ) ;
#61273=AXIS2_PLACEMENT_3D ( 'NONE', #142940, #68283, #111750 ) ;
#61274=DIRECTION ( 'NONE',  ( 0.6830127018922180770, -0.6830127018922204085, -0.2588190451025213501 ) ) ;
#61276=VECTOR ( 'NONE', #66728, 1000.000000000000000 ) ;
#61277=EDGE_LOOP ( 'NONE', ( #5352, #94767, #109921, #76428 ) ) ;
#61278=EDGE_CURVE ( 'NONE', #88187, #130377, #12133, .T. ) ;
#61279=DIRECTION ( 'NONE',  ( -0.6830127018922180770, -0.6830127018922202975, -0.2588190451025213501 ) ) ;
#61282=CARTESIAN_POINT ( 'NONE',  ( 66.48921356237309510, -27.52281430457101763, 5.000000000000000000 ) ) ;
#61283=CARTESIAN_POINT ( 'NONE',  ( -34.92500000000001137, 1.800094516027185065, 4.759050581649336031 ) ) ;
#61284=VERTEX_POINT ( 'NONE', #100599 ) ;
#61285=ORIENTED_EDGE ( 'NONE', *, *, #45562, .T. ) ;
#61289=ORIENTED_EDGE ( 'NONE', *, *, #60849, .T. ) ;
#61290=EDGE_LOOP ( 'NONE', ( #11483, #90898, #98995, #123464 ) ) ;
#61291=VECTOR ( 'NONE', #22241, 1000.000000000000000 ) ;
#61292=DIRECTION ( 'NONE',  ( 0.7071067811865487940, -0.7071067811865463515, 0.000000000000000000 ) ) ;
#61293=VECTOR ( 'NONE', #102430, 1000.000000000000114 ) ;
#61295=CARTESIAN_POINT ( 'NONE',  ( -34.92500000000001137, 22.22500000000000142, 4.000000000000000000 ) ) ;
#61296=DIRECTION ( 'NONE',  ( -0.000000000000000000, 0.3543493200069153248, 0.9351131265310292928 ) ) ;
#61297=FACE_BOUND ( 'NONE', #123536, .T. ) ;
#61298=DIRECTION ( 'NONE',  ( 0.7071067811865486830, -0.7071067811865464625, -0.000000000000000000 ) ) ;
#61299=DIRECTION ( 'NONE',  ( -0.7071067811865486830, 0.7071067811865464625, 0.000000000000000000 ) ) ;
#61300=DIRECTION ( 'NONE',  ( 0.7071067811865486830, -0.7071067811865464625, -0.000000000000000000 ) ) ;
#61301=EDGE_LOOP ( 'NONE', ( #97845, #36493, #49323, #73226 ) ) ;
#61302=VECTOR ( 'NONE', #10120, 999.9999999999998863 ) ;
#61304=ORIENTED_EDGE ( 'NONE', *, *, #43242, .T. ) ;
#61308=ORIENTED_EDGE ( 'NONE', *, *, #139821, .T. ) ;
#61310=ORIENTED_EDGE ( 'NONE', *, *, #75131, .T. ) ;
#61311=VECTOR ( 'NONE', #134003, 1000.000000000000000 ) ;
#61312=CARTESIAN_POINT ( 'NONE',  ( 34.49999999999975842, 1.030536316426539756, -5.498701923753880116 ) ) ;
#61313=CARTESIAN_POINT ( 'NONE',  ( 72.48921356237309510, -27.52281430457106026, 5.000000000000000000 ) ) ;
#61314=CARTESIAN_POINT ( 'NONE',  ( -17.20710678118642889, -20.24070752338407075, 5.000000000000000000 ) ) ;
#61315=CARTESIAN_POINT ( 'NONE',  ( -28.49999999999980815, -17.56887692260762535, 4.000000000000000000 ) ) ;
#61316=ORIENTED_EDGE ( 'NONE', *, *, #62982, .T. ) ;
#61318=CARTESIAN_POINT ( 'NONE',  ( 66.29974487139159578, -27.71228299555252406, 4.000000000000000000 ) ) ;
#61319=CARTESIAN_POINT ( 'NONE',  ( -27.70710678118634718, 17.25929247661554555, 5.000000000000000000 ) ) ;
#61320=CARTESIAN_POINT ( 'NONE',  ( -60.48921356237309510, -27.52281430457097500, 5.000000000000000000 ) ) ;
#61321=CARTESIAN_POINT ( 'NONE',  ( 0.000000000000000000, 0.000000000000000000, 5.000000000000000000 ) ) ;
#61322=CARTESIAN_POINT ( 'NONE',  ( 2.999999999999992450, 17.58746187583906107, 4.000000000000000000 ) ) ;
#61323=CARTESIAN_POINT ( 'NONE',  ( -36.18398860626899705, 28.73617430169812437, 5.000000000000000000 ) ) ;
#61324=LINE ( 'NONE', #128668, #56214 ) ;
#61325=ORIENTED_EDGE ( 'NONE', *, *, #84598, .F. ) ;
#61326=DIRECTION ( 'NONE',  ( -0.7071067811865486830, 0.7071067811865464625, 0.000000000000000000 ) ) ;
#61327=PLANE ( 'NONE',  #39604 ) ;
#61328=ORIENTED_EDGE ( 'NONE', *, *, #77386, .T. ) ;
#61329=ORIENTED_EDGE ( 'NONE', *, *, #86200, .F. ) ;
#61330=ORIENTED_EDGE ( 'NONE', *, *, #28178, .F. ) ;
#61332=ORIENTED_EDGE ( 'NONE', *, *, #7669, .T. ) ;
#61335=EDGE_LOOP ( 'NONE', ( #70786, #19222, #133502 ) ) ;
#61336=CARTESIAN_POINT ( 'NONE',  ( 17.70025512860841488, -27.71228299555193786, 4.000000000000000000 ) ) ;
#61337=ORIENTED_EDGE ( 'NONE', *, *, #104730, .F. ) ;
#61338=DIRECTION ( 'NONE',  ( -0.7071067811865487940, 0.7071067811865463515, 0.000000000000000000 ) ) ;
#61340=CARTESIAN_POINT ( 'NONE',  ( 24.70701326429286482, -21.74070752338406365, 4.999753212805220670 ) ) ;
#61341=ORIENTED_EDGE ( 'NONE', *, *, #1344, .F. ) ;
#61342=ORIENTED_EDGE ( 'NONE', *, *, #110263, .F. ) ;
#61343=VECTOR ( 'NONE', #103507, 1000.000000000000227 ) ;
#61344=DIRECTION ( 'NONE',  ( -0.7071067811865486830, -0.7071067811865464625, 0.000000000000000000 ) ) ;
#61345=CARTESIAN_POINT ( 'NONE',  ( 20.99451991528748707, 28.92564299267952777, 4.000000000000000000 ) ) ;
#61346=ORIENTED_EDGE ( 'NONE', *, *, #107026, .T. ) ;
#61347=DIRECTION ( 'NONE',  ( 0.6830127018922181881, 0.6830127018922202975, -0.2588190451025214056 ) ) ;
#61348=ORIENTED_EDGE ( 'NONE', *, *, #102947, .F. ) ;
#61349=VERTEX_POINT ( 'NONE', #103417 ) ;
#61351=EDGE_LOOP ( 'NONE', ( #76051, #54432, #69016, #133675 ) ) ;
#61352=ADVANCED_FACE ( 'NONE', ( #69401 ), #80987, .F. ) ;
#61353=DIRECTION ( 'NONE',  ( -0.7071067811865486830, -0.7071067811865464625, 0.000000000000000000 ) ) ;
#61354=DIRECTION ( 'NONE',  ( -0.7071067811865487940, 0.7071067811865463515, 0.000000000000000000 ) ) ;
#61355=ADVANCED_FACE ( 'NONE', ( #102014 ), #113587, .F. ) ;
#61358=ADVANCED_FACE ( 'NONE', ( #13545 ), #4782, .F. ) ;
#61359=ADVANCED_FACE ( 'NONE', ( #25878 ), #92537, .F. ) ;
#61362=EDGE_LOOP ( 'NONE', ( #116927, #53014, #26816, #63547 ) ) ;
#61363=DIRECTION ( 'NONE',  ( -0.7071067811865486830, -0.7071067811865464625, 0.000000000000000000 ) ) ;
#61364=EDGE_CURVE ( 'NONE', #62795, #103277, #70150, .T. ) ;
#61365=EDGE_CURVE ( 'NONE', #51943, #3084, #102738, .T. ) ;
#61366=AXIS2_PLACEMENT_3D ( 'NONE', #110727, #65877, #131814 ) ;
#61368=CARTESIAN_POINT ( 'NONE',  ( -34.49999999999975842, -13.53574439159936915, 4.994342998332166772 ) ) ;
#61369=DIRECTION ( 'NONE',  ( -0.6830127018922180770, -0.6830127018922204085, -0.2588190451025213501 ) ) ;
#61370=CARTESIAN_POINT ( 'NONE',  ( 10.49999999999992539, -4.216083040037235996, -7.486842126848680223 ) ) ;
#61373=ORIENTED_EDGE ( 'NONE', *, *, #21080, .F. ) ;
#61374=EDGE_CURVE ( 'NONE', #61485, #6222, #136775, .T. ) ;
#61380=LINE ( 'NONE', #105525, #35911 ) ;
#61383=CARTESIAN_POINT ( 'NONE',  ( -33.18398860626899705, 28.73617430169810305, 5.000000000000000000 ) ) ;
#61384=EDGE_CURVE ( 'NONE', #101064, #137064, #114988, .T. ) ;
#61385=LINE ( 'NONE', #4030, #96917 ) ;
#61386=CARTESIAN_POINT ( 'NONE',  ( 7.499999999999947597, 11.52377502935403619, -1.522421517564102267 ) ) ;
#61387=DIRECTION ( 'NONE',  ( 0.7071067811865486830, -0.7071067811865464625, -0.000000000000000000 ) ) ;
#61388=DIRECTION ( 'NONE',  ( 0.7071067811865487940, 0.7071067811865463515, 0.000000000000000000 ) ) ;
#61389=ORIENTED_EDGE ( 'NONE', *, *, #87274, .T. ) ;
#61390=DIRECTION ( 'NONE',  ( -0.6830127018922181881, 0.6830127018922202975, -0.2588190451025214056 ) ) ;
#61391=EDGE_LOOP ( 'NONE', ( #36234, #88786, #28542, #60778 ) ) ;
#61392=EDGE_CURVE ( 'NONE', #61677, #140803, #101294, .T. ) ;
#61393=DIRECTION ( 'NONE',  ( 0.7071067811865486830, -0.7071067811865464625, -0.000000000000000000 ) ) ;
#61394=CARTESIAN_POINT ( 'NONE',  ( -9.792893218813388145, 0.7592924766157104211, 5.000000000000000000 ) ) ;
#61395=ORIENTED_EDGE ( 'NONE', *, *, #69542, .F. ) ;
#61396=DIRECTION ( 'NONE',  ( -0.7071067811865486830, -0.7071067811865464625, 0.000000000000000000 ) ) ;
#61397=DIRECTION ( 'NONE',  ( -0.6830127018922181881, 0.6830127018922202975, -0.2588190451025214056 ) ) ;
#61400=CARTESIAN_POINT ( 'NONE',  ( 12.79289321881337216, 6.759292476615651246, 5.000000000000000000 ) ) ;
#61401=EDGE_CURVE ( 'NONE', #10796, #37388, #35362, .T. ) ;
#61402=CARTESIAN_POINT ( 'NONE',  ( 5.287690060339683029, -21.73547319004781642, 4.999917730833664642 ) ) ;
#61403=VECTOR ( 'NONE', #87412, 1000.000000000000000 ) ;
#61405=CARTESIAN_POINT ( 'NONE',  ( 6.489213562373093325, -27.52281430457059841, 5.000000000000000000 ) ) ;
#61406=VECTOR ( 'NONE', #28508, 1000.000000000000000 ) ;
#61408=DIRECTION ( 'NONE',  ( 0.7071067811865487940, 0.7071067811865463515, 0.000000000000000000 ) ) ;
#61409=ORIENTED_EDGE ( 'NONE', *, *, #14611, .T. ) ;
#61412=FACE_OUTER_BOUND ( 'NONE', #113803, .T. ) ;
#61414=ADVANCED_FACE ( 'NONE', ( #134667 ), #123790, .F. ) ;
#61415=LINE ( 'NONE', #14986, #134794 ) ;
#61416=DIRECTION ( 'NONE',  ( -0.7071067811865486830, 0.7071067811865464625, 0.000000000000000000 ) ) ;
#61417=VERTEX_POINT ( 'NONE', #39642 ) ;
#61419=EDGE_CURVE ( 'NONE', #87121, #31173, #72697, .T. ) ;
#61422=EDGE_CURVE ( 'NONE', #22237, #126442, #116459, .T. ) ;
#61423=CARTESIAN_POINT ( 'NONE',  ( -51.29974487139158867, -27.71228299555242103, 4.000000000000000000 ) ) ;
#61424=LINE ( 'NONE', #82421, #121006 ) ;
#61425=FACE_OUTER_BOUND ( 'NONE', #104772, .T. ) ;
#61428=EDGE_CURVE ( 'NONE', #12779, #25917, #83868, .T. ) ;
#61429=DIRECTION ( 'NONE',  ( -1.000000000000000000, 0.000000000000000000, 0.000000000000000000 ) ) ;
#61430=LINE ( 'NONE', #105570, #138874 ) ;
#61432=EDGE_LOOP ( 'NONE', ( #49165, #79385, #28950, #78584 ) ) ;
#61434=CARTESIAN_POINT ( 'NONE',  ( -19.00193056682084247, -22.22500000000000142, 4.500000000000000888 ) ) ;
#61436=EDGE_CURVE ( 'NONE', #7238, #55692, #106998, .T. ) ;
#61437=CARTESIAN_POINT ( 'NONE',  ( -34.49999999999976552, 19.39370406404964342, 1.459788787078281080 ) ) ;
#61438=EDGE_LOOP ( 'NONE', ( #23400, #11496, #9493, #141199 ) ) ;
#61439=VERTEX_POINT ( 'NONE', #7678 ) ;
#61441=VERTEX_POINT ( 'NONE', #21247 ) ;
#61442=ADVANCED_FACE ( 'NONE', ( #128758 ), #17150, .F. ) ;
#61443=LINE ( 'NONE', #81758, #103129 ) ;
#61444=CARTESIAN_POINT ( 'NONE',  ( -34.49999999999976552, 1.464255608400471642, 4.994342998332163219 ) ) ;
#61445=LINE ( 'NONE', #105587, #43443 ) ;
#61447=DIRECTION ( 'NONE',  ( -0.000000000000000000, 0.000000000000000000, 1.000000000000000000 ) ) ;
#61450=EDGE_CURVE ( 'NONE', #31939, #142484, #50496, .T. ) ;
#61451=CARTESIAN_POINT ( 'NONE',  ( -11.99999999999992362, 2.342191155542436842, -5.001666872980057299 ) ) ;
#61452=CARTESIAN_POINT ( 'NONE',  ( 27.79289321881327268, -20.24070752338406720, 5.000000000000000000 ) ) ;
#61453=LINE ( 'NONE', #95454, #118699 ) ;
#61454=ORIENTED_EDGE ( 'NONE', *, *, #293, .T. ) ;
#61455=EDGE_LOOP ( 'NONE', ( #138813, #99169, #26341, #106038 ) ) ;
#61456=EDGE_CURVE ( 'NONE', #133319, #54084, #6221, .T. ) ;
#61457=DIRECTION ( 'NONE',  ( -0.000000000000000000, -0.3543493200069152693, 0.9351131265310292928 ) ) ;
#61458=LINE ( 'NONE', #18588, #34627 ) ;
#61460=CARTESIAN_POINT ( 'NONE',  ( -3.005480084712505828, 28.92564299267936079, 4.000000000000000000 ) ) ;
#61462=CIRCLE ( 'NONE', #47596, 5.968999999999998529 ) ;
#61464=VERTEX_POINT ( 'NONE', #51934 ) ;
#61465=ORIENTED_EDGE ( 'NONE', *, *, #27152, .F. ) ;
#61467=ORIENTED_EDGE ( 'NONE', *, *, #34508, .F. ) ;
#61468=( BOUNDED_CURVE ( )  B_SPLINE_CURVE ( 3, ( #31037, #120868, #96943, #65101 ),
 .UNSPECIFIED., .F., .F. ) 
 B_SPLINE_CURVE_WITH_KNOTS ( ( 4, 4 ),
 ( 1.862445515227526327, 1.909667095125054725 ),
 .UNSPECIFIED. ) 
 CURVE ( )  GEOMETRIC_REPRESENTATION_ITEM ( )  RATIONAL_B_SPLINE_CURVE ( ( 1.000000000000000000, 0.9998141854983972898, 0.9998141854983972898, 1.000000000000000000 ) ) 
 REPRESENTATION_ITEM ( '' )  );
#61470=DIRECTION ( 'NONE',  ( -0.7071067811865486830, -0.7071067811865464625, 0.000000000000000000 ) ) ;
#61471=DIRECTION ( 'NONE',  ( -0.7071067811865486830, -0.7071067811865464625, 0.000000000000000000 ) ) ;
#61472=EDGE_CURVE ( 'NONE', #110860, #56431, #105558, .T. ) ;
#61473=ORIENTED_EDGE ( 'NONE', *, *, #421, .F. ) ;
#61474=VECTOR ( 'NONE', #127676, 1000.000000000000000 ) ;
#61476=FACE_OUTER_BOUND ( 'NONE', #84480, .T. ) ;
#61477=CARTESIAN_POINT ( 'NONE',  ( 34.75611968250419181, -7.294349301475873126, 4.955485411084881164 ) ) ;
#61480=ORIENTED_EDGE ( 'NONE', *, *, #82196, .T. ) ;
#61481=CARTESIAN_POINT ( 'NONE',  ( 33.77004279457769798, 21.73644205237998506, 5.000000000000000888 ) ) ;
#61483=ORIENTED_EDGE ( 'NONE', *, *, #120997, .F. ) ;
#61484=CARTESIAN_POINT ( 'NONE',  ( 16.49999999999988631, -7.420205493532884056, -2.617629953481214855 ) ) ;
#61485=VERTEX_POINT ( 'NONE', #27288 ) ;
#61486=EDGE_CURVE ( 'NONE', #43835, #133600, #72294, .T. ) ;
#61487=CARTESIAN_POINT ( 'NONE',  ( 39.18398860626899705, 28.73617430169814568, 5.000000000000000000 ) ) ;
#61488=ORIENTED_EDGE ( 'NONE', *, *, #42185, .F. ) ;
#61489=ORIENTED_EDGE ( 'NONE', *, *, #7147, .F. ) ;
#61491=ORIENTED_EDGE ( 'NONE', *, *, #93308, .F. ) ;
#61493=CARTESIAN_POINT ( 'NONE',  ( -68.99451991528748351, 28.92564299267986172, 4.000000000000000000 ) ) ;
#61494=AXIS2_PLACEMENT_3D ( 'NONE', #115181, #60893, #60155 ) ;
#61495=DIRECTION ( 'NONE',  ( -0.6830127018922180770, -0.6830127018922204085, -0.2588190451025213501 ) ) ;
#61497=DIRECTION ( 'NONE',  ( 0.7071067811865487940, 0.7071067811865463515, 0.000000000000000000 ) ) ;
#61498=AXIS2_PLACEMENT_3D ( 'NONE', #5622, #104954, #39735 ) ;
#61499=FACE_OUTER_BOUND ( 'NONE', #119736, .T. ) ;
#61500=DIRECTION ( 'NONE',  ( -0.7071067811865486830, 0.7071067811865464625, 0.000000000000000000 ) ) ;
#61501=DIRECTION ( 'NONE',  ( -0.7071067811865486830, -0.7071067811865464625, 0.000000000000000000 ) ) ;
#61502=VECTOR ( 'NONE', #91139, 1000.000000000000227 ) ;
#61503=LINE ( 'NONE', #117942, #95581 ) ;
#61505=CARTESIAN_POINT ( 'NONE',  ( -36.29974487139159578, -27.71228299555231445, 4.000000000000000000 ) ) ;
#61506=ORIENTED_EDGE ( 'NONE', *, *, #1729, .F. ) ;
#61510=EDGE_CURVE ( 'NONE', #33459, #42329, #40355, .T. ) ;
#61511=FACE_OUTER_BOUND ( 'NONE', #34104, .T. ) ;
#61512=VERTEX_POINT ( 'NONE', #29434 ) ;
#61513=LINE ( 'NONE', #130321, #53712 ) ;
#61516=CARTESIAN_POINT ( 'NONE',  ( 34.49999999999975842, 12.05432934483081908, 4.994342998332162331 ) ) ;
#61517=EDGE_CURVE ( 'NONE', #129569, #75615, #71543, .T. ) ;
#61518=ORIENTED_EDGE ( 'NONE', *, *, #132480, .T. ) ;
#61520=ORIENTED_EDGE ( 'NONE', *, *, #137199, .F. ) ;
#61522=ADVANCED_FACE ( 'NONE', ( #73000 ), #49808, .F. ) ;
#61524=LINE ( 'NONE', #105672, #139580 ) ;
#61525=EDGE_CURVE ( 'NONE', #68726, #61837, #38901, .T. ) ;
#61526=CARTESIAN_POINT ( 'NONE',  ( 3.299744871391591339, -27.71228299555208352, 4.000000000000000000 ) ) ;
#61529=ORIENTED_EDGE ( 'NONE', *, *, #131011, .T. ) ;
#61530=ADVANCED_FACE ( 'NONE', ( #106259 ), #139675, .F. ) ;
#61531=EDGE_LOOP ( 'NONE', ( #134554, #112647, #20186, #95439 ) ) ;
#61532=LINE ( 'NONE', #30287, #88931 ) ;
#61533=CARTESIAN_POINT ( 'NONE',  ( 34.49999999999976552, -14.94567065516889848, 4.994342998332158778 ) ) ;
#61534=DIRECTION ( 'NONE',  ( -0.7071067811865486830, -0.7071067811865464625, 0.000000000000000000 ) ) ;
#61536=CARTESIAN_POINT ( 'NONE',  ( 54.18398860626899705, 28.73617430169825226, 5.000000000000000000 ) ) ;
#61537=CARTESIAN_POINT ( 'NONE',  ( 23.99999999999983302, -7.068876922607743474, 4.000000000000000000 ) ) ;
#61538=EDGE_CURVE ( 'NONE', #135668, #78193, #24815, .T. ) ;
#61539=PLANE ( 'NONE',  #127268 ) ;
#61540=CARTESIAN_POINT ( 'NONE',  ( 20.66652290003515446, 8.920938975803856863, 4.000000000000000000 ) ) ;
#61541=ORIENTED_EDGE ( 'NONE', *, *, #116955, .F. ) ;
#61542=DIRECTION ( 'NONE',  ( -0.3543493200069162685, -0.000000000000000000, -0.9351131265310288487 ) ) ;
#61543=DIRECTION ( 'NONE',  ( -0.000000000000000000, 0.3543493200069153248, 0.9351131265310292928 ) ) ;
#61544=ORIENTED_EDGE ( 'NONE', *, *, #85869, .T. ) ;
#61545=EDGE_CURVE ( 'NONE', #25035, #60374, #132902, .T. ) ;
#61546=DIRECTION ( 'NONE',  ( -0.7071067811865486830, 0.7071067811865464625, 0.000000000000000000 ) ) ;
#61549=EDGE_CURVE ( 'NONE', #65537, #99825, #78494, .T. ) ;
#61550=CARTESIAN_POINT ( 'NONE',  ( 26.29289321881327268, 8.259292476615639700, 5.000000000000000000 ) ) ;
#61551=DIRECTION ( 'NONE',  ( 0.6830127018922180770, -0.6830127018922204085, -0.2588190451025213501 ) ) ;
#61553=CARTESIAN_POINT ( 'NONE',  ( 17.99999999999989342, 20.58746187583903620, 4.000000000000000000 ) ) ;
#61554=ORIENTED_EDGE ( 'NONE', *, *, #137481, .T. ) ;
#61555=EDGE_CURVE ( 'NONE', #117394, #99025, #101658, .T. ) ;
#61556=PLANE ( 'NONE',  #84536 ) ;
#61557=VECTOR ( 'NONE', #117354, 1000.000000000000000 ) ;
#61559=CARTESIAN_POINT ( 'NONE',  ( 13.82816939922342669, -8.240707523384203981, 4.000000000000000000 ) ) ;
#61560=DIRECTION ( 'NONE',  ( -0.3543493200069162685, -0.000000000000000000, -0.9351131265310288487 ) ) ;
#61561=VECTOR ( 'NONE', #202, 1000.000000000000000 ) ;
#61562=CARTESIAN_POINT ( 'NONE',  ( 0.000000000000000000, 0.000000000000000000, 5.000000000000000000 ) ) ;
#61563=CARTESIAN_POINT ( 'NONE',  ( 59.99451991528749772, 28.92564299267980132, 4.000000000000000000 ) ) ;
#61564=DIRECTION ( 'NONE',  ( 0.6830127018922181881, 0.6830127018922202975, -0.2588190451025214056 ) ) ;
#61567=DIRECTION ( 'NONE',  ( -0.7071067811865487940, 0.7071067811865463515, 0.000000000000000000 ) ) ;
#61568=FACE_OUTER_BOUND ( 'NONE', #96344, .T. ) ;
#61569=CARTESIAN_POINT ( 'NONE',  ( 4.748455871324219757, -11.24070752338416490, 10.39518518046008211 ) ) ;
#61570=ORIENTED_EDGE ( 'NONE', *, *, #102124, .T. ) ;
#61571=ORIENTED_EDGE ( 'NONE', *, *, #45467, .F. ) ;
#61574=ORIENTED_EDGE ( 'NONE', *, *, #136347, .T. ) ;
#61575=EDGE_CURVE ( 'NONE', #11390, #99127, #90060, .T. ) ;
#61577=DIRECTION ( 'NONE',  ( 1.000000000000000000, -0.000000000000000000, -0.000000000000000000 ) ) ;
#61578=CARTESIAN_POINT ( 'NONE',  ( 3.469446951953614189E-15, -8.731860332648842871, -2.120594902707538143 ) ) ;
#61579=ORIENTED_EDGE ( 'NONE', *, *, #11682, .T. ) ;
#61580=CARTESIAN_POINT ( 'NONE',  ( 15.70710678118643955, -3.740707523384239952, 5.000000000000000000 ) ) ;
#61581=PLANE ( 'NONE',  #62635 ) ;
#61582=CARTESIAN_POINT ( 'NONE',  ( -5.292893218813418343, -6.740707523384218192, 5.000000000000000000 ) ) ;
#61583=DIRECTION ( 'NONE',  ( 1.000000000000000000, 0.000000000000000000, 0.000000000000000000 ) ) ;
#61584=CARTESIAN_POINT ( 'NONE',  ( 17.51078643762690845, -27.52281430457043143, 5.000000000000000000 ) ) ;
#61585=DIRECTION ( 'NONE',  ( 0.000000000000000000, -1.000000000000000000, 0.000000000000000000 ) ) ;
#61586=FACE_OUTER_BOUND ( 'NONE', #80557, .T. ) ;
#61587=LINE ( 'NONE', #18006, #75540 ) ;
#61589=EDGE_CURVE ( 'NONE', #119359, #7710, #90811, .T. ) ;
#61590=VECTOR ( 'NONE', #107727, 1000.000000000000227 ) ;
#61592=ORIENTED_EDGE ( 'NONE', *, *, #71873, .T. ) ;
#61593=ORIENTED_EDGE ( 'NONE', *, *, #33033, .F. ) ;
#61594=VECTOR ( 'NONE', #125606, 999.9999999999998863 ) ;
#61596=ORIENTED_EDGE ( 'NONE', *, *, #66462, .T. ) ;
#61597=AXIS2_PLACEMENT_3D ( 'NONE', #19177, #140252, #8262 ) ;
#61599=EDGE_CURVE ( 'NONE', #48649, #15762, #13201, .T. ) ;
#61601=VECTOR ( 'NONE', #38529, 1000.000000000000000 ) ;
#61602=CARTESIAN_POINT ( 'NONE',  ( -18.29974487139159223, -27.71228299555219010, 4.000000000000000000 ) ) ;
#61604=CARTESIAN_POINT ( 'NONE',  ( -57.48921356237308800, -27.52281430457095368, 5.000000000000000000 ) ) ;
#61605=FACE_OUTER_BOUND ( 'NONE', #113978, .T. ) ;
#61607=VERTEX_POINT ( 'NONE', #46633 ) ;
#61608=EDGE_CURVE ( 'NONE', #57945, #81077, #900, .T. ) ;
#61609=CARTESIAN_POINT ( 'NONE',  ( 17.28769006033959954, -21.73547319004781286, 4.999917730833664642 ) ) ;
#61610=ORIENTED_EDGE ( 'NONE', *, *, #58959, .F. ) ;
#61611=PLANE ( 'NONE',  #96251 ) ;
#61612=DIRECTION ( 'NONE',  ( 1.000000000000000000, 0.000000000000000000, 0.000000000000000000 ) ) ;
#61613=DIRECTION ( 'NONE',  ( 0.7071067811865487940, -0.7071067811865463515, 0.000000000000000000 ) ) ;
#61614=LINE ( 'NONE', #2349, #138847 ) ;
#61615=ORIENTED_EDGE ( 'NONE', *, *, #36040, .F. ) ;
#61617=EDGE_CURVE ( 'NONE', #53079, #77276, #98790, .T. ) ;
#61620=PLANE ( 'NONE',  #75506 ) ;
#61622=CARTESIAN_POINT ( 'NONE',  ( -21.18398860626899349, 28.73617430169802134, 5.000000000000000000 ) ) ;
#61623=( NAMED_UNIT ( * ) PLANE_ANGLE_UNIT ( ) SI_UNIT ( $, .RADIAN. ) );
#61624=ORIENTED_EDGE ( 'NONE', *, *, #136456, .T. ) ;
#61625=EDGE_LOOP ( 'NONE', ( #59191, #97391, #59402, #9861 ) ) ;
#61626=PLANE ( 'NONE',  #101281 ) ;
#61627=ORIENTED_EDGE ( 'NONE', *, *, #1573, .T. ) ;
#61628=ORIENTED_EDGE ( 'NONE', *, *, #1166, .F. ) ;
#61629=VECTOR ( 'NONE', #44084, 1000.000000000000000 ) ;
#61631=FACE_OUTER_BOUND ( 'NONE', #47034, .T. ) ;
#61632=LINE ( 'NONE', #115220, #12487 ) ;
#61633=ADVANCED_FACE ( 'NONE', ( #24114 ), #32869, .F. ) ;
#61635=LINE ( 'NONE', #105789, #94628 ) ;
#61636=CARTESIAN_POINT ( 'NONE',  ( -7.499999999999944045, -10.04351517176479014, -1.623559851933840337 ) ) ;
#61638=DIRECTION ( 'NONE',  ( -0.7071067811865487940, 0.7071067811865463515, 0.000000000000000000 ) ) ;
#61640=ORIENTED_EDGE ( 'NONE', *, *, #103290, .T. ) ;
#61642=CARTESIAN_POINT ( 'NONE',  ( 14.99999999999989519, 9.631307414974335401, -9.079085613539508159 ) ) ;
#61643=CARTESIAN_POINT ( 'NONE',  ( -26.99999999999980815, 19.55218569542896390, 5.000000000000000000 ) ) ;
#61644=ADVANCED_FACE ( 'NONE', ( #133596 ), #77090, .F. ) ;
#61645=ORIENTED_EDGE ( 'NONE', *, *, #130693, .T. ) ;
#61647=VERTEX_POINT ( 'NONE', #11773 ) ;
#61649=( BOUNDED_CURVE ( )  B_SPLINE_CURVE ( 3, ( #134302, #53902, #90053, #67640 ),
 .UNSPECIFIED., .F., .T. ) 
 B_SPLINE_CURVE_WITH_KNOTS ( ( 4, 4 ),
 ( 5.106027341939277875, 6.645403452391244414 ),
 .UNSPECIFIED. ) 
 CURVE ( )  GEOMETRIC_REPRESENTATION_ITEM ( )  RATIONAL_B_SPLINE_CURVE ( ( 1.000000000000000000, 0.8120851936182275077, 0.8120851936182275077, 1.000000000000000000 ) ) 
 REPRESENTATION_ITEM ( '' )  );
#61650=ORIENTED_EDGE ( 'NONE', *, *, #87367, .T. ) ;
#61653=LINE ( 'NONE', #138481, #55279 ) ;
#61656=CARTESIAN_POINT ( 'NONE',  ( -41.99451991528749062, 28.92564299267967343, 4.000000000000000000 ) ) ;
#61658=FACE_OUTER_BOUND ( 'NONE', #92413, .T. ) ;
#61659=DIRECTION ( 'NONE',  ( -0.000000000000000000, 0.3543493200069153248, 0.9351131265310292928 ) ) ;
#61660=FACE_OUTER_BOUND ( 'NONE', #52755, .T. ) ;
#61661=LINE ( 'NONE', #29697, #76036 ) ;
#61662=FACE_OUTER_BOUND ( 'NONE', #21848, .T. ) ;
#61663=CIRCLE ( 'NONE', #142672, 5.968999999999998529 ) ;
#61664=VERTEX_POINT ( 'NONE', #57475 ) ;
#61665=ORIENTED_EDGE ( 'NONE', *, *, #39053, .F. ) ;
#61666=ORIENTED_EDGE ( 'NONE', *, *, #134560, .F. ) ;
#61667=VERTEX_POINT ( 'NONE', #100943 ) ;
#61671=DIRECTION ( 'NONE',  ( -0.000000000000000000, 0.000000000000000000, 1.000000000000000000 ) ) ;
#61672=CARTESIAN_POINT ( 'NONE',  ( -35.99451991528749772, 28.92564299267963079, 4.000000000000000000 ) ) ;
#61673=VECTOR ( 'NONE', #36780, 999.9999999999998863 ) ;
#61674=CARTESIAN_POINT ( 'NONE',  ( -32.99999999999976552, 13.55218569542903140, 5.000000000000000000 ) ) ;
#61676=DIRECTION ( 'NONE',  ( 0.7071067811865487940, 0.7071067811865463515, 0.000000000000000000 ) ) ;
#61677=VERTEX_POINT ( 'NONE', #111841 ) ;
#61678=VECTOR ( 'NONE', #7523, 1000.000000000000227 ) ;
#61679=AXIS2_PLACEMENT_3D ( 'NONE', #109722, #24148, #54649 ) ;
#61680=CARTESIAN_POINT ( 'NONE',  ( 54.29974487139159578, -27.71228299555243879, 4.000000000000000000 ) ) ;
#61681=DIRECTION ( 'NONE',  ( -0.000000000000000000, 0.000000000000000000, 1.000000000000000000 ) ) ;
#61682=ADVANCED_FACE ( 'NONE', ( #110373 ), #100245, .F. ) ;
#61684=EDGE_LOOP ( 'NONE', ( #142619, #69495, #138429, #23983 ) ) ;
#61686=DIRECTION ( 'NONE',  ( -0.3543493200069162685, -0.000000000000000000, -0.9351131265310288487 ) ) ;
#61687=EDGE_CURVE ( 'NONE', #104985, #114666, #77786, .T. ) ;
#61688=CARTESIAN_POINT ( 'NONE',  ( -45.48921356237309510, -27.52281430457087197, 5.000000000000000000 ) ) ;
#61689=EDGE_LOOP ( 'NONE', ( #75856, #109993, #48264, #136510 ) ) ;
#61690=ORIENTED_EDGE ( 'NONE', *, *, #70095, .F. ) ;
#61691=EDGE_CURVE ( 'NONE', #74078, #50218, #34273, .T. ) ;
#61692=CARTESIAN_POINT ( 'NONE',  ( 21.18398860626899349, 28.73617430169802134, 5.000000000000000000 ) ) ;
#61693=ORIENTED_EDGE ( 'NONE', *, *, #101440, .T. ) ;
#61694=CARTESIAN_POINT ( 'NONE',  ( -12.70710678118645731, -3.740707523384243505, 5.000000000000000000 ) ) ;
#61695=LINE ( 'NONE', #7248, #48789 ) ;
#61696=CARTESIAN_POINT ( 'NONE',  ( 0.000000000000000000, 21.72500000000000142, 4.500000000000000888 ) ) ;
#61697=EDGE_CURVE ( 'NONE', #94785, #3074, #67648, .T. ) ;
#61698=DIRECTION ( 'NONE',  ( -0.7071067811865487940, 0.7071067811865463515, -0.000000000000000000 ) ) ;
#61699=ORIENTED_EDGE ( 'NONE', *, *, #133464, .T. ) ;
#61700=CARTESIAN_POINT ( 'NONE',  ( -9.299744871391588674, -27.71228299555212971, 4.000000000000000000 ) ) ;
#61701=LINE ( 'NONE', #5830, #25599 ) ;
#61703=ORIENTED_EDGE ( 'NONE', *, *, #23331, .T. ) ;
#61704=LINE ( 'NONE', #47294, #55920 ) ;
#61705=CARTESIAN_POINT ( 'NONE',  ( 56.99451991528749062, 28.92564299267978001, 4.000000000000000000 ) ) ;
#61707=EDGE_CURVE ( 'NONE', #99872, #81380, #92926, .T. ) ;
#61708=CARTESIAN_POINT ( 'NONE',  ( -5.510786437626906675, -27.52281430457051314, 5.000000000000000000 ) ) ;
#61709=ORIENTED_EDGE ( 'NONE', *, *, #46487, .T. ) ;
#61710=EDGE_CURVE ( 'NONE', #78277, #86576, #61074, .T. ) ;
#61711=ORIENTED_EDGE ( 'NONE', *, *, #115960, .T. ) ;
#61712=CARTESIAN_POINT ( 'NONE',  ( -31.49999999999977263, -17.94781430457064531, 5.000000000000000000 ) ) ;
#61713=FACE_OUTER_BOUND ( 'NONE', #125280, .T. ) ;
#61714=ORIENTED_EDGE ( 'NONE', *, *, #121114, .F. ) ;
#61715=CARTESIAN_POINT ( 'NONE',  ( 2.816011393730999401, 28.73617430169785436, 5.000000000000000000 ) ) ;
#61717=CARTESIAN_POINT ( 'NONE',  ( 24.48921356237309510, -27.52281430457072631, 5.000000000000000000 ) ) ;
#61718=VECTOR ( 'NONE', #143479, 1000.000000000000000 ) ;
#61719=CARTESIAN_POINT ( 'NONE',  ( 8.999999999999937828, -19.44781430457063465, 5.000000000000000000 ) ) ;
#61720=DIRECTION ( 'NONE',  ( -0.6830127018922180770, -0.6830127018922204085, -0.2588190451025213501 ) ) ;
#61721=CARTESIAN_POINT ( 'NONE',  ( -12.72281430457050710, -21.72500000000000142, 5.000000000000000000 ) ) ;
#61723=CARTESIAN_POINT ( 'NONE',  ( 6.489213562373093325, -27.52281430457059841, 5.000000000000000000 ) ) ;
#61724=EDGE_CURVE ( 'NONE', #130915, #76045, #58938, .T. ) ;
#61725=DIRECTION ( 'NONE',  ( 0.7071067811865486830, -0.7071067811865464625, -0.000000000000000000 ) ) ;
#61726=VECTOR ( 'NONE', #28941, 1000.000000000000000 ) ;
#61727=DIRECTION ( 'NONE',  ( -0.7071067811865486830, 0.7071067811865464625, 0.000000000000000000 ) ) ;
#61728=DIRECTION ( 'NONE',  ( -0.000000000000000000, 0.000000000000000000, 1.000000000000000000 ) ) ;
#61729=CARTESIAN_POINT ( 'NONE',  ( -12.18398860626900060, 28.73617430169795739, 5.000000000000000000 ) ) ;
#61731=ORIENTED_EDGE ( 'NONE', *, *, #114669, .F. ) ;
#61732=ORIENTED_EDGE ( 'NONE', *, *, #4457, .F. ) ;
#61734=ORIENTED_EDGE ( 'NONE', *, *, #27693, .F. ) ;
#61735=ORIENTED_EDGE ( 'NONE', *, *, #20414, .T. ) ;
#61736=ORIENTED_EDGE ( 'NONE', *, *, #142016, .F. ) ;
#61738=VECTOR ( 'NONE', #102554, 999.9999999999998863 ) ;
#61739=DIRECTION ( 'NONE',  ( -0.7071067811865486830, -0.7071067811865464625, 0.000000000000000000 ) ) ;
#61740=DIRECTION ( 'NONE',  ( 0.7071067811865486830, -0.7071067811865464625, -0.000000000000000000 ) ) ;
#61743=DIRECTION ( 'NONE',  ( 0.3543493200069163240, 0.000000000000000000, -0.9351131265310288487 ) ) ;
#61744=CARTESIAN_POINT ( 'NONE',  ( -42.48921356237308800, -27.52281430457085065, 5.000000000000000000 ) ) ;
#61750=LINE ( 'NONE', #95049, #82154 ) ;
#61753=DIRECTION ( 'NONE',  ( -0.7071067811865486830, 0.7071067811865464625, 0.000000000000000000 ) ) ;
#61755=EDGE_CURVE ( 'NONE', #131987, #37298, #58216, .T. ) ;
#61756=VECTOR ( 'NONE', #44551, 1000.000000000000227 ) ;
#61757=DIRECTION ( 'NONE',  ( 0.6830127018922180770, -0.6830127018922204085, -0.2588190451025213501 ) ) ;
#61758=LINE ( 'NONE', #125582, #66950 ) ;
#61760=ORIENTED_EDGE ( 'NONE', *, *, #58108, .F. ) ;
#61762=VECTOR ( 'NONE', #121654, 1000.000000000000000 ) ;
#61763=ORIENTED_EDGE ( 'NONE', *, *, #139385, .T. ) ;
#61764=DIRECTION ( 'NONE',  ( -0.6830127018922180770, -0.6830127018922204085, -0.2588190451025213501 ) ) ;
#61766=PLANE ( 'NONE',  #119778 ) ;
#61768=DIRECTION ( 'NONE',  ( 0.7071067811865486830, -0.7071067811865464625, -0.000000000000000000 ) ) ;
#61770=VECTOR ( 'NONE', #39699, 999.9999999999998863 ) ;
#61771=ORIENTED_EDGE ( 'NONE', *, *, #9284, .T. ) ;
#61772=EDGE_CURVE ( 'NONE', #98208, #67296, #137883, .T. ) ;
#61773=CARTESIAN_POINT ( 'NONE',  ( 18.29974487139159223, -27.71228299555219010, 4.000000000000000000 ) ) ;
#61774=VERTEX_POINT ( 'NONE', #38557 ) ;
#61775=LINE ( 'NONE', #29121, #60148 ) ;
#61776=CARTESIAN_POINT ( 'NONE',  ( -8.207106781186478628, -11.24070752338416845, 5.000000000000000000 ) ) ;
#61777=DIRECTION ( 'NONE',  ( 0.6830127018922181881, 0.6830127018922202975, -0.2588190451025214056 ) ) ;
#61778=PLANE ( 'NONE',  #4671 ) ;
#61781=EDGE_CURVE ( 'NONE', #116410, #101064, #50155, .T. ) ;
#61782=VERTEX_POINT ( 'NONE', #3054 ) ;
#61783=CARTESIAN_POINT ( 'NONE',  ( -11.99999999999990585, 2.587461875839209391, 4.000000000000000000 ) ) ;
#61784=CARTESIAN_POINT ( 'NONE',  ( -10.49999999999992184, -5.947814304570770538, 5.000000000000000000 ) ) ;
#61785=CYLINDRICAL_SURFACE ( 'NONE', #84942, 0.5000000000000000000 ) ;
#61787=AXIS2_PLACEMENT_3D ( 'NONE', #129151, #63915, #108081 ) ;
#61788=VECTOR ( 'NONE', #125434, 1000.000000000000000 ) ;
#61790=VECTOR ( 'NONE', #44473, 1000.000000000000000 ) ;
#61793=DIRECTION ( 'NONE',  ( 1.000000000000000000, 0.000000000000000000, 0.000000000000000000 ) ) ;
#61794=EDGE_CURVE ( 'NONE', #74659, #87168, #39281, .T. ) ;
#61795=LINE ( 'NONE', #30582, #36310 ) ;
#61797=ORIENTED_EDGE ( 'NONE', *, *, #19423, .T. ) ;
#61798=AXIS2_PLACEMENT_3D ( 'NONE', #126769, #105719, #28198 ) ;
#61799=DIRECTION ( 'NONE',  ( -1.000000000000000000, -8.718663809566799855E-16, 0.000000000000000000 ) ) ;
#61803=ADVANCED_FACE ( 'NONE', ( #83504 ), #124843, .F. ) ;
#61806=PLANE ( 'NONE',  #141449 ) ;
#61807=EDGE_CURVE ( 'NONE', #132626, #19726, #103100, .T. ) ;
#61808=FACE_BOUND ( 'NONE', #3151, .T. ) ;
#61809=DIRECTION ( 'NONE',  ( 0.7071067811865486830, -0.7071067811865464625, -0.000000000000000000 ) ) ;
#61811=CARTESIAN_POINT ( 'NONE',  ( -11.24139925780195171, 21.72500000000000142, 5.000000000000000000 ) ) ;
#61812=EDGE_CURVE ( 'NONE', #118545, #68539, #127719, .T. ) ;
#61813=ORIENTED_EDGE ( 'NONE', *, *, #28768, .F. ) ;
#61814=PLANE ( 'NONE',  #105918 ) ;
#61815=LINE ( 'NONE', #72727, #22687 ) ;
#61816=EDGE_LOOP ( 'NONE', ( #102644, #40626, #13071, #85389 ) ) ;
#61817=CIRCLE ( 'NONE', #75775, 5.968999999999998529 ) ;
#61818=ORIENTED_EDGE ( 'NONE', *, *, #96029, .T. ) ;
#61820=ORIENTED_EDGE ( 'NONE', *, *, #55459, .T. ) ;
#61823=ORIENTED_EDGE ( 'NONE', *, *, #67709, .F. ) ;
#61824=LINE ( 'NONE', #61147, #115840 ) ;
#61827=DIRECTION ( 'NONE',  ( -1.000000000000000000, 0.000000000000000000, -0.000000000000000000 ) ) ;
#61829=ADVANCED_FACE ( 'NONE', ( #48025 ), #37118, .F. ) ;
#61830=PLANE ( 'NONE',  #112740 ) ;
#61831=CARTESIAN_POINT ( 'NONE',  ( 14.72063736826143732, 7.288814752023356824, 4.957798599204235046 ) ) ;
#61833=CARTESIAN_POINT ( 'NONE',  ( -26.99999999999980105, 4.552185695429119328, 5.000000000000000000 ) ) ;
#61834=FACE_OUTER_BOUND ( 'NONE', #132820, .T. ) ;
#61835=ORIENTED_EDGE ( 'NONE', *, *, #62820, .T. ) ;
#61836=VECTOR ( 'NONE', #65316, 1000.000000000000227 ) ;
#61837=VERTEX_POINT ( 'NONE', #4416 ) ;
#61838=LINE ( 'NONE', #8797, #77182 ) ;
#61839=DIRECTION ( 'NONE',  ( -0.000000000000000000, 0.000000000000000000, 1.000000000000000000 ) ) ;
#61840=ORIENTED_EDGE ( 'NONE', *, *, #111043, .F. ) ;
#61842=ORIENTED_EDGE ( 'NONE', *, *, #23184, .F. ) ;
#61843=CARTESIAN_POINT ( 'NONE',  ( -63.18398860626900415, 28.73617430169831621, 5.000000000000000000 ) ) ;
#61845=AXIS2_PLACEMENT_3D ( 'NONE', #87101, #31999, #98674 ) ;
#61847=ORIENTED_EDGE ( 'NONE', *, *, #60542, .F. ) ;
#61848=CARTESIAN_POINT ( 'NONE',  ( 23.99451991528749062, 28.92564299267954908, 4.000000000000000000 ) ) ;
#61850=EDGE_CURVE ( 'NONE', #138986, #136777, #82784, .T. ) ;
#61852=ADVANCED_FACE ( 'NONE', ( #82096 ), #126970, .F. ) ;
#61853=DIRECTION ( 'NONE',  ( -0.7071067811865486830, -0.7071067811865464625, -0.000000000000000000 ) ) ;
#61854=ORIENTED_EDGE ( 'NONE', *, *, #112766, .F. ) ;
#61855=DIRECTION ( 'NONE',  ( 1.000000000000000000, 0.000000000000000000, 0.000000000000000000 ) ) ;
#61856=AXIS2_PLACEMENT_3D ( 'NONE', #43954, #141096, #8410 ) ;
#61860=DIRECTION ( 'NONE',  ( 0.7071067811865487940, 0.7071067811865463515, 0.000000000000000000 ) ) ;
#61861=EDGE_LOOP ( 'NONE', ( #94171, #122202, #44140, #6740 ) ) ;
#61862=FACE_OUTER_BOUND ( 'NONE', #75554, .T. ) ;
#61863=ORIENTED_EDGE ( 'NONE', *, *, #2387, .T. ) ;
#61864=CARTESIAN_POINT ( 'NONE',  ( -24.70710678118636494, -3.740707523384241728, 5.000000000000000000 ) ) ;
#61865=CARTESIAN_POINT ( 'NONE',  ( 23.99999999999983302, -12.41253812416062274, 4.000000000000000000 ) ) ;
#61866=EDGE_CURVE ( 'NONE', #5681, #43625, #5170, .T. ) ;
#61869=ORIENTED_EDGE ( 'NONE', *, *, #33403, .F. ) ;
#61870=CARTESIAN_POINT ( 'NONE',  ( 6.793339364578431017, 21.75929247661549226, 4.998822639870705409 ) ) ;
#61871=CARTESIAN_POINT ( 'NONE',  ( -24.48921356237309510, -27.52281430457072631, 5.000000000000000000 ) ) ;
#61872=FACE_OUTER_BOUND ( 'NONE', #40457, .T. ) ;
#61873=ORIENTED_EDGE ( 'NONE', *, *, #2716, .T. ) ;
#61874=FACE_OUTER_BOUND ( 'NONE', #127702, .T. ) ;
#61876=PLANE ( 'NONE',  #58569 ) ;
#61877=DIRECTION ( 'NONE',  ( -0.7071067811865486830, 0.7071067811865464625, 0.000000000000000000 ) ) ;
#61878=ADVANCED_FACE ( 'NONE', ( #30545 ), #84908, .T. ) ;
#61879=CARTESIAN_POINT ( 'NONE',  ( -27.32816939922334143, -0.7407075233842683737, 4.000000000000000000 ) ) ;
#61880=ORIENTED_EDGE ( 'NONE', *, *, #120898, .F. ) ;
#61883=DIRECTION ( 'NONE',  ( 0.000000000000000000, -1.000000000000000000, 0.000000000000000000 ) ) ;
#61884=CARTESIAN_POINT ( 'NONE',  ( 0.7999687798316279519, 8.259292476615634371, 16.85664084051840916 ) ) ;
#61885=VECTOR ( 'NONE', #53700, 1000.000000000000000 ) ;
#61886=AXIS2_PLACEMENT_3D ( 'NONE', #44138, #10057, #54324 ) ;
#61888=FACE_OUTER_BOUND ( 'NONE', #12824, .T. ) ;
#61890=DIRECTION ( 'NONE',  ( -0.7071067811865487940, 0.7071067811865463515, -0.000000000000000000 ) ) ;
#61891=ADVANCED_FACE ( 'NONE', ( #53733 ), #95780, .F. ) ;
#61893=ORIENTED_EDGE ( 'NONE', *, *, #70651, .F. ) ;
#61894=PLANE ( 'NONE',  #71957 ) ;
#61895=LINE ( 'NONE', #28544, #99869 ) ;
#61896=LINE ( 'NONE', #118373, #5317 ) ;
#61897=VECTOR ( 'NONE', #22651, 1000.000000000000000 ) ;
#61898=EDGE_CURVE ( 'NONE', #13412, #110421, #9453, .T. ) ;
#61899=DIRECTION ( 'NONE',  ( 1.000000000000000000, 0.000000000000000000, 0.000000000000000000 ) ) ;
#61902=VERTEX_POINT ( 'NONE', #118957 ) ;
#61903=LINE ( 'NONE', #95208, #81375 ) ;
#61904=VERTEX_POINT ( 'NONE', #63891 ) ;
#61906=EDGE_CURVE ( 'NONE', #83991, #81813, #18185, .T. ) ;
#61909=LINE ( 'NONE', #140848, #80837 ) ;
#61910=CARTESIAN_POINT ( 'NONE',  ( 34.92499999999998295, 22.22500000000000142, 4.500000000000000888 ) ) ;
#61911=PLANE ( 'NONE',  #13958 ) ;
#61912=DIRECTION ( 'NONE',  ( -0.000000000000000000, -0.000000000000000000, 1.000000000000000000 ) ) ;
#61914=ORIENTED_EDGE ( 'NONE', *, *, #27960, .F. ) ;
#61915=EDGE_CURVE ( 'NONE', #74246, #126135, #18933, .T. ) ;
#61916=LINE ( 'NONE', #8187, #9352 ) ;
#61917=DIRECTION ( 'NONE',  ( 0.7071067811865487940, 0.7071067811865463515, -0.000000000000000000 ) ) ;
#61918=VECTOR ( 'NONE', #67005, 1000.000000000000000 ) ;
#61919=EDGE_CURVE ( 'NONE', #82657, #79851, #118226, .T. ) ;
#61920=DIRECTION ( 'NONE',  ( -0.6830127018922181881, 0.6830127018922202975, -0.2588190451025214056 ) ) ;
#61923=CARTESIAN_POINT ( 'NONE',  ( -28.49999999999980460, -2.568876922607784774, 4.000000000000000000 ) ) ;
#61926=VECTOR ( 'NONE', #114444, 1000.000000000000000 ) ;
#61927=CARTESIAN_POINT ( 'NONE',  ( -3.516654386410431599, 22.22500000000000142, 4.500000000000000888 ) ) ;
#61928=ORIENTED_EDGE ( 'NONE', *, *, #96054, .T. ) ;
#61929=ORIENTED_EDGE ( 'NONE', *, *, #40357, .F. ) ;
#61932=DIRECTION ( 'NONE',  ( -0.7071067811865486830, -0.7071067811865464625, 0.000000000000000000 ) ) ;
#61933=VECTOR ( 'NONE', #37522, 1000.000000000000000 ) ;
#61934=CARTESIAN_POINT ( 'NONE',  ( -14.99451991528749595, 28.92564299267948513, 4.000000000000000000 ) ) ;
#61935=ORIENTED_EDGE ( 'NONE', *, *, #99420, .T. ) ;
#61936=EDGE_CURVE ( 'NONE', #93683, #134564, #64589, .T. ) ;
#61937=CARTESIAN_POINT ( 'NONE',  ( 0.4892135623730947680, -27.52281430457055578, 5.000000000000000000 ) ) ;
#61938=LINE ( 'NONE', #83698, #81410 ) ;
#61940=ORIENTED_EDGE ( 'NONE', *, *, #29127, .F. ) ;
#61941=VECTOR ( 'NONE', #45010, 1000.000000000000000 ) ;
#61942=DIRECTION ( 'NONE',  ( -0.3543493200069162685, -0.000000000000000000, -0.9351131265310288487 ) ) ;
#61943=EDGE_LOOP ( 'NONE', ( #113075, #119475, #52196, #142438 ) ) ;
#61944=EDGE_LOOP ( 'NONE', ( #19869, #1422, #125221, #33047 ) ) ;
#61945=FACE_OUTER_BOUND ( 'NONE', #98764, .T. ) ;
#61946=DIRECTION ( 'NONE',  ( -0.7071067811865487940, 0.7071067811865463515, -0.000000000000000000 ) ) ;
#61947=PLANE ( 'NONE',  #139277 ) ;
#61948=VECTOR ( 'NONE', #89767, 1000.000000000000227 ) ;
#61949=LINE ( 'NONE', #126447, #71821 ) ;
#61950=CARTESIAN_POINT ( 'NONE',  ( 57.18398860626899705, 28.73617430169827358, 5.000000000000000000 ) ) ;
#61952=VERTEX_POINT ( 'NONE', #8037 ) ;
#61956=ORIENTED_EDGE ( 'NONE', *, *, #110691, .T. ) ;
#61957=ORIENTED_EDGE ( 'NONE', *, *, #45413, .T. ) ;
#61960=DIRECTION ( 'NONE',  ( 0.3543493200069162685, -0.000000000000000000, -0.9351131265310288487 ) ) ;
#61961=CARTESIAN_POINT ( 'NONE',  ( -34.49999999999974420, -20.94567065516883275, 4.994342998332162331 ) ) ;
#61962=ADVANCED_FACE ( 'NONE', ( #96461 ), #140703, .F. ) ;
#61964=DIRECTION ( 'NONE',  ( 0.3543493200069164351, 2.781805975412904658E-17, -0.9351131265310288487 ) ) ;
#61966=ORIENTED_EDGE ( 'NONE', *, *, #128395, .F. ) ;
#61967=EDGE_LOOP ( 'NONE', ( #23054, #52941, #50554, #14369 ) ) ;
#61968=LINE ( 'NONE', #38068, #70108 ) ;
#61969=CARTESIAN_POINT ( 'NONE',  ( -34.42500000000001137, 8.977185695429334089, 5.000000000000000000 ) ) ;
#61970=ORIENTED_EDGE ( 'NONE', *, *, #91994, .T. ) ;
#61971=VERTEX_POINT ( 'NONE', #97934 ) ;
#61972=CARTESIAN_POINT ( 'NONE',  ( 22.63753812416082667, 22.22500000000000142, 4.000000000000000000 ) ) ;
#61973=ORIENTED_EDGE ( 'NONE', *, *, #137370, .F. ) ;
#61975=CARTESIAN_POINT ( 'NONE',  ( 34.92499999999997584, 4.800094516027123781, 4.759050581649322709 ) ) ;
#61976=AXIS2_PLACEMENT_3D ( 'NONE', #126025, #26698, #104224 ) ;
#61977=CIRCLE ( 'NONE', #68919, 5.968999999999998529 ) ;
#61978=ADVANCED_FACE ( 'NONE', ( #131272 ), #31959, .F. ) ;
#61979=FACE_BOUND ( 'NONE', #63458, .T. ) ;
#61980=LINE ( 'NONE', #40234, #59482 ) ;
#61981=DIRECTION ( 'NONE',  ( -0.3543493200069163240, -0.000000000000000000, -0.9351131265310288487 ) ) ;
#61984=CARTESIAN_POINT ( 'NONE',  ( -66.48921356237309510, -27.52281430457101763, 5.000000000000000000 ) ) ;
#61989=CARTESIAN_POINT ( 'NONE',  ( 2.999999999999981792, 4.384688058510572972, -7.090945410444678743 ) ) ;
#61991=VERTEX_POINT ( 'NONE', #40016 ) ;
#61992=VECTOR ( 'NONE', #63732, 1000.000000000000000 ) ;
#61993=ORIENTED_EDGE ( 'NONE', *, *, #78718, .F. ) ;
#61995=ORIENTED_EDGE ( 'NONE', *, *, #134644, .F. ) ;
#61996=DIRECTION ( 'NONE',  ( 1.000000000000000000, 0.000000000000000000, 0.000000000000000000 ) ) ;
#61997=EDGE_CURVE ( 'NONE', #41151, #115678, #129843, .T. ) ;
#61998=LINE ( 'NONE', #126493, #118334 ) ;
#61999=LINE ( 'NONE', #141687, #18929 ) ;
#62000=EDGE_CURVE ( 'NONE', #63781, #121984, #106913, .T. ) ;
#62001=FACE_OUTER_BOUND ( 'NONE', #11460, .T. ) ;
#62002=ORIENTED_EDGE ( 'NONE', *, *, #23717, .F. ) ;
#62004=DIRECTION ( 'NONE',  ( -0.7071067811865487940, 0.7071067811865463515, 0.000000000000000000 ) ) ;
#62005=CARTESIAN_POINT ( 'NONE',  ( -6.793339364578430128, 21.75929247661548871, 4.998822639870703632 ) ) ;
#62006=CARTESIAN_POINT ( 'NONE',  ( -42.18398860626899705, 28.73617430169816700, 5.000000000000000000 ) ) ;
#62008=EDGE_CURVE ( 'NONE', #96838, #18115, #51586, .T. ) ;
#62009=DIRECTION ( 'NONE',  ( -0.6830127018922181881, 0.6830127018922202975, -0.2588190451025214056 ) ) ;
#62010=EDGE_LOOP ( 'NONE', ( #136378, #135548, #6109, #83618 ) ) ;
#62011=CARTESIAN_POINT ( 'NONE',  ( -15.29974487139158867, -27.71228299555216879, 4.000000000000000000 ) ) ;
#62012=CARTESIAN_POINT ( 'NONE',  ( 42.48921356237308800, -27.52281430457085065, 5.000000000000000000 ) ) ;
#62013=VERTEX_POINT ( 'NONE', #132001 ) ;
#62014=EDGE_LOOP ( 'NONE', ( #79832, #24493, #80149, #103625 ) ) ;
#62015=ORIENTED_EDGE ( 'NONE', *, *, #43829, .T. ) ;
#62017=VECTOR ( 'NONE', #50401, 999.9999999999998863 ) ;
#62018=EDGE_CURVE ( 'NONE', #80143, #107445, #112383, .T. ) ;
#62019=ORIENTED_EDGE ( 'NONE', *, *, #54303, .F. ) ;
#62020=VECTOR ( 'NONE', #131182, 999.9999999999998863 ) ;
#62022=( BOUNDED_CURVE ( )  B_SPLINE_CURVE ( 3, ( #106759, #63315, #142967, #74155 ),
 .UNSPECIFIED., .F., .T. ) 
 B_SPLINE_CURVE_WITH_KNOTS ( ( 4, 4 ),
 ( 4.350170835173026163, 4.500739107949210727 ),
 .UNSPECIFIED. ) 
 CURVE ( )  GEOMETRIC_REPRESENTATION_ITEM ( )  RATIONAL_B_SPLINE_CURVE ( ( 1.000000000000000000, 0.9981116584018956406, 0.9981116584018956406, 1.000000000000000000 ) ) 
 REPRESENTATION_ITEM ( '' )  );
#62024=ORIENTED_EDGE ( 'NONE', *, *, #73537, .F. ) ;
#62025=CARTESIAN_POINT ( 'NONE',  ( 18.63311396761903538, -2.779424156541560276, 4.000000000000000000 ) ) ;
#62026=EDGE_CURVE ( 'NONE', #41817, #126052, #109517, .T. ) ;
#62027=ORIENTED_EDGE ( 'NONE', *, *, #51874, .T. ) ;
#62028=CARTESIAN_POINT ( 'NONE',  ( -24.79593897580385331, 4.791522900035168675, 4.000000000000000000 ) ) ;
#62029=CARTESIAN_POINT ( 'NONE',  ( 34.49999999999975842, -2.945670655169024155, 4.994342998332159667 ) ) ;
#62030=DIRECTION ( 'NONE',  ( -0.7071067811865486830, 0.7071067811865464625, 0.000000000000000000 ) ) ;
#62033=CARTESIAN_POINT ( 'NONE',  ( -11.51078643762690490, -27.52281430457047406, 5.000000000000000000 ) ) ;
#62035=EDGE_CURVE ( 'NONE', #78067, #73712, #43548, .T. ) ;
#62037=ORIENTED_EDGE ( 'NONE', *, *, #77957, .T. ) ;
#62038=DIRECTION ( 'NONE',  ( -0.000000000000000000, 0.3543493200069153248, 0.9351131265310292928 ) ) ;
#62039=ORIENTED_EDGE ( 'NONE', *, *, #37742, .F. ) ;
#62040=ORIENTED_EDGE ( 'NONE', *, *, #97011, .F. ) ;
#62043=CARTESIAN_POINT ( 'NONE',  ( 15.48921356237309510, -27.52281430457066236, 5.000000000000000000 ) ) ;
#62045=LINE ( 'NONE', #72236, #51633 ) ;
#62046=CARTESIAN_POINT ( 'NONE',  ( 3.469446951953614189E-15, -12.03360074219761700, 5.000000000000000000 ) ) ;
#62047=EDGE_CURVE ( 'NONE', #59037, #94354, #54455, .T. ) ;
#62048=CARTESIAN_POINT ( 'NONE',  ( 23.99999999999981881, -13.39766691384881803, -10.96608748226471697 ) ) ;
#62049=VERTEX_POINT ( 'NONE', #120348 ) ;
#62050=EDGE_CURVE ( 'NONE', #79253, #46769, #68207, .T. ) ;
#62051=LINE ( 'NONE', #6883, #129994 ) ;
#62053=DIRECTION ( 'NONE',  ( -0.000000000000000000, -0.3543493200069152693, 0.9351131265310292928 ) ) ;
#62054=DIRECTION ( 'NONE',  ( 1.000000000000000000, 0.000000000000000000, 0.000000000000000000 ) ) ;
#62056=ORIENTED_EDGE ( 'NONE', *, *, #98301, .F. ) ;
#62057=DIRECTION ( 'NONE',  ( -0.7071067811865487940, 0.7071067811865463515, -0.000000000000000000 ) ) ;
#62058=VECTOR ( 'NONE', #124022, 1000.000000000000000 ) ;
#62059=EDGE_CURVE ( 'NONE', #69770, #84967, #101489, .T. ) ;
#62061=ORIENTED_EDGE ( 'NONE', *, *, #2759, .F. ) ;
#62062=ORIENTED_EDGE ( 'NONE', *, *, #35654, .T. ) ;
#62063=VERTEX_POINT ( 'NONE', #57314 ) ;
#62064=DIRECTION ( 'NONE',  ( -0.000000000000000000, 0.000000000000000000, 1.000000000000000000 ) ) ;
#62065=DIRECTION ( 'NONE',  ( -0.3543493200069162685, -0.000000000000000000, -0.9351131265310288487 ) ) ;
#62067=EDGE_CURVE ( 'NONE', #98083, #109689, #110912, .T. ) ;
#62070=LINE ( 'NONE', #4029, #34881 ) ;
#62071=CARTESIAN_POINT ( 'NONE',  ( 0.000000000000000000, 0.000000000000000000, 5.000000000000000000 ) ) ;
#62072=LINE ( 'NONE', #141021, #20990 ) ;
#62073=DIRECTION ( 'NONE',  ( -0.7071067811865487940, 0.7071067811865463515, 0.000000000000000000 ) ) ;
#62075=ORIENTED_EDGE ( 'NONE', *, *, #57881, .F. ) ;
#62077=ORIENTED_EDGE ( 'NONE', *, *, #70327, .T. ) ;
#62078=AXIS2_PLACEMENT_3D ( 'NONE', #37410, #125861, #26532 ) ;
#62079=CARTESIAN_POINT ( 'NONE',  ( 32.99999999999976552, 9.631307414974347836, -9.079085613539465527 ) ) ;
#62080=DIRECTION ( 'NONE',  ( 1.000000000000000000, -0.000000000000000000, -0.000000000000000000 ) ) ;
#62081=ORIENTED_EDGE ( 'NONE', *, *, #15872, .T. ) ;
#62082=VECTOR ( 'NONE', #90125, 1000.000000000000000 ) ;
#62083=CARTESIAN_POINT ( 'NONE',  ( 3.156123077392388065, -22.22500000000000142, 4.000000000000000000 ) ) ;
#62084=DIRECTION ( 'NONE',  ( -0.3543493200069162685, -0.000000000000000000, -0.9351131265310288487 ) ) ;
#62085=ORIENTED_EDGE ( 'NONE', *, *, #122030, .F. ) ;
#62086=EDGE_LOOP ( 'NONE', ( #128714, #132849, #5606, #141594 ) ) ;
#62087=CARTESIAN_POINT ( 'NONE',  ( -33.48921356237309510, -27.52281430457078670, 5.000000000000000000 ) ) ;
#62089=VECTOR ( 'NONE', #42580, 1000.000000000000000 ) ;
#62090=VECTOR ( 'NONE', #11480, 1000.000000000000227 ) ;
#62091=DIRECTION ( 'NONE',  ( -0.3543493200069163240, 4.681814790819596721E-17, -0.9351131265310288487 ) ) ;
#62095=CARTESIAN_POINT ( 'NONE',  ( 25.82816939922335209, -14.24070752338412937, 4.000000000000000000 ) ) ;
#62096=ORIENTED_EDGE ( 'NONE', *, *, #131237, .T. ) ;
#62098=LINE ( 'NONE', #38200, #4375 ) ;
#62100=DIRECTION ( 'NONE',  ( 0.7071067811865487940, -0.7071067811865463515, 0.000000000000000000 ) ) ;
#62101=ORIENTED_EDGE ( 'NONE', *, *, #49876, .F. ) ;
#62102=CARTESIAN_POINT ( 'NONE',  ( 22.41489890804854568, -1.755427004171022709, 4.190031470807595859 ) ) ;
#62103=ORIENTED_EDGE ( 'NONE', *, *, #66247, .F. ) ;
#62106=CARTESIAN_POINT ( 'NONE',  ( -4.069960254864057880, -0.7407075233842770334, 13.87443053587611708 ) ) ;
#62107=CARTESIAN_POINT ( 'NONE',  ( -36.29974487139159578, -27.71228299555231445, 4.000000000000000000 ) ) ;
#62108=EDGE_LOOP ( 'NONE', ( #132879, #126158, #2593, #105433 ) ) ;
#62110=CARTESIAN_POINT ( 'NONE',  ( -34.92500000000001137, 22.22500000000000142, 4.000000000000000000 ) ) ;
#62111=DIRECTION ( 'NONE',  ( -0.7071067811865486830, -0.7071067811865464625, 0.000000000000000000 ) ) ;
#62112=PLANE ( 'NONE',  #137806 ) ;
#62114=DIRECTION ( 'NONE',  ( 0.7071067811865487940, 0.7071067811865463515, -0.000000000000000000 ) ) ;
#62115=VECTOR ( 'NONE', #49707, 1000.000000000000227 ) ;
#62116=CARTESIAN_POINT ( 'NONE',  ( 10.03163515922185844, 2.259292476615701428, 13.77329220150639522 ) ) ;
#62118=CARTESIAN_POINT ( 'NONE',  ( -57.18398860626899705, 28.73617430169827358, 5.000000000000000000 ) ) ;
#62119=ORIENTED_EDGE ( 'NONE', *, *, #44779, .F. ) ;
#62120=ORIENTED_EDGE ( 'NONE', *, *, #23410, .T. ) ;
#62122=ORIENTED_EDGE ( 'NONE', *, *, #127417, .F. ) ;
#62124=EDGE_CURVE ( 'NONE', #50272, #61349, #65336, .T. ) ;
#62125=LINE ( 'NONE', #18569, #101293 ) ;
#62126=CARTESIAN_POINT ( 'NONE',  ( -5.510786437626906675, -27.52281430457051314, 5.000000000000000000 ) ) ;
#62128=VECTOR ( 'NONE', #108657, 1000.000000000000000 ) ;
#62129=CARTESIAN_POINT ( 'NONE',  ( 0.000000000000000000, 0.000000000000000000, 5.000000000000000000 ) ) ;
#62130=LINE ( 'NONE', #83903, #81429 ) ;
#62132=ADVANCED_FACE ( 'NONE', ( #99329 ), #98630, .F. ) ;
#62133=ORIENTED_EDGE ( 'NONE', *, *, #17903, .F. ) ;
#62134=CARTESIAN_POINT ( 'NONE',  ( -42.18398860626899705, 28.73617430169816700, 5.000000000000000000 ) ) ;
#62135=CARTESIAN_POINT ( 'NONE',  ( 0.000000000000000000, 0.000000000000000000, 5.000000000000000000 ) ) ;
#62136=DIRECTION ( 'NONE',  ( -0.000000000000000000, 0.3543493200069153248, 0.9351131265310292928 ) ) ;
#62137=ORIENTED_EDGE ( 'NONE', *, *, #21118, .F. ) ;
#62138=ORIENTED_EDGE ( 'NONE', *, *, #75562, .F. ) ;
#62139=EDGE_CURVE ( 'NONE', #22706, #7595, #77628, .T. ) ;
#62140=ADVANCED_FACE ( 'NONE', ( #134142 ), #56389, .T. ) ;
#62142=CARTESIAN_POINT ( 'NONE',  ( -57.29974487139158157, -27.71228299555246011, 4.000000000000000000 ) ) ;
#62144=LINE ( 'NONE', #138992, #11819 ) ;
#62146=DIRECTION ( 'NONE',  ( -0.000000000000000000, -0.3543493200069152138, 0.9351131265310292928 ) ) ;
#62148=ADVANCED_FACE ( 'NONE', ( #111667 ), #91363, .F. ) ;
#62149=CARTESIAN_POINT ( 'NONE',  ( 20.99999999999986855, 20.96639925780205616, 5.000000000000000000 ) ) ;
#62151=EDGE_LOOP ( 'NONE', ( #21992, #46601, #20381, #34802 ) ) ;
#62152=ORIENTED_EDGE ( 'NONE', *, *, #117610, .F. ) ;
#62153=AXIS2_PLACEMENT_3D ( 'NONE', #132079, #53050, #131346 ) ;
#62154=ORIENTED_EDGE ( 'NONE', *, *, #27763, .F. ) ;
#62155=EDGE_CURVE ( 'NONE', #6816, #38440, #4250, .T. ) ;
#62157=CARTESIAN_POINT ( 'NONE',  ( 63.29974487139158867, -27.71228299555250274, 4.000000000000000000 ) ) ;
#62158=EDGE_CURVE ( 'NONE', #131471, #83058, #47181, .T. ) ;
#62160=FACE_OUTER_BOUND ( 'NONE', #83356, .T. ) ;
#62161=DIRECTION ( 'NONE',  ( 1.000000000000000000, 0.000000000000000000, 0.000000000000000000 ) ) ;
#62162=VECTOR ( 'NONE', #103717, 1000.000000000000000 ) ;
#62163=DIRECTION ( 'NONE',  ( -0.000000000000000000, -0.3543493200069152693, 0.9351131265310292928 ) ) ;
#62164=DIRECTION ( 'NONE',  ( -0.7071067811865486830, -0.7071067811865464625, -0.000000000000000000 ) ) ;
#62165=AXIS2_PLACEMENT_3D ( 'NONE', #51286, #72357, #48412 ) ;
#62169=FACE_OUTER_BOUND ( 'NONE', #131426, .T. ) ;
#62170=DIRECTION ( 'NONE',  ( -0.6830127018922181881, 0.6830127018922202975, -0.2588190451025214056 ) ) ;
#62172=ORIENTED_EDGE ( 'NONE', *, *, #71672, .F. ) ;
#62173=DIRECTION ( 'NONE',  ( 0.7071067811865486830, -0.7071067811865464625, -0.000000000000000000 ) ) ;
#62174=ORIENTED_EDGE ( 'NONE', *, *, #56140, .F. ) ;
#62175=VECTOR ( 'NONE', #118718, 1000.000000000000000 ) ;
#62176=DIRECTION ( 'NONE',  ( 0.7071067811865487940, 0.7071067811865463515, -0.000000000000000000 ) ) ;
#62177=ORIENTED_EDGE ( 'NONE', *, *, #62155, .T. ) ;
#62179=ADVANCED_FACE ( 'NONE', ( #82600 ), #60156, .T. ) ;
#62180=AXIS2_PLACEMENT_3D ( 'NONE', #97833, #99980, #10789 ) ;
#62181=ORIENTED_EDGE ( 'NONE', *, *, #7285, .F. ) ;
#62182=VECTOR ( 'NONE', #127, 1000.000000000000000 ) ;
#62183=VECTOR ( 'NONE', #69788, 999.9999999999998863 ) ;
#62186=DIRECTION ( 'NONE',  ( -0.6830127018922180770, -0.6830127018922204085, -0.2588190451025213501 ) ) ;
#62187=ADVANCED_FACE ( 'NONE', ( #4988 ), #3576, .F. ) ;
#62188=FACE_OUTER_BOUND ( 'NONE', #37079, .T. ) ;
#62189=DIRECTION ( 'NONE',  ( 0.3543493200069162685, -0.000000000000000000, -0.9351131265310288487 ) ) ;
#62190=VECTOR ( 'NONE', #40826, 1000.000000000000000 ) ;
#62191=DIRECTION ( 'NONE',  ( -0.6830127018922181881, 0.6830127018922202975, -0.2588190451025214056 ) ) ;
#62192=CARTESIAN_POINT ( 'NONE',  ( 23.99999999999983302, -10.77435723561691994, -9.972017380717284496 ) ) ;
#62194=ADVANCED_FACE ( 'NONE', ( #104322 ), #102234, .F. ) ;
#62195=ORIENTED_EDGE ( 'NONE', *, *, #38779, .T. ) ;
#62196=VECTOR ( 'NONE', #60860, 1000.000000000000000 ) ;
#62197=CARTESIAN_POINT ( 'NONE',  ( -36.18398860626899705, 28.73617430169812437, 5.000000000000000000 ) ) ;
#62199=VERTEX_POINT ( 'NONE', #137711 ) ;
#62201=VERTEX_POINT ( 'NONE', #81929 ) ;
#62202=CIRCLE ( 'NONE', #80733, 3.378199999999994319 ) ;
#62204=ORIENTED_EDGE ( 'NONE', *, *, #91967, .F. ) ;
#62205=VECTOR ( 'NONE', #4934, 1000.000000000000000 ) ;
#62207=DIRECTION ( 'NONE',  ( -0.6830127018922180770, -0.6830127018922204085, -0.2588190451025213501 ) ) ;
#62208=DIRECTION ( 'NONE',  ( 0.7071067811865487940, 0.7071067811865463515, 0.000000000000000000 ) ) ;
#62211=DIRECTION ( 'NONE',  ( -0.000000000000000000, 0.000000000000000000, 1.000000000000000000 ) ) ;
#62212=ORIENTED_EDGE ( 'NONE', *, *, #100311, .F. ) ;
#62214=ORIENTED_EDGE ( 'NONE', *, *, #80448, .T. ) ;
#62217=DIRECTION ( 'NONE',  ( 0.7071067811865486830, -0.7071067811865464625, -0.000000000000000000 ) ) ;
#62218=DIRECTION ( 'NONE',  ( 0.7071067811865486830, -0.7071067811865464625, -0.000000000000000000 ) ) ;
#62220=CARTESIAN_POINT ( 'NONE',  ( -9.299744871391588674, -27.71228299555212971, 4.000000000000000000 ) ) ;
#62221=VERTEX_POINT ( 'NONE', #128952 ) ;
#62222=ORIENTED_EDGE ( 'NONE', *, *, #19624, .F. ) ;
#62223=EDGE_LOOP ( 'NONE', ( #133432, #26974, #12048, #26717 ) ) ;
#62224=DIRECTION ( 'NONE',  ( 0.7071067811865487940, 0.7071067811865463515, 0.000000000000000000 ) ) ;
#62225=DIRECTION ( 'NONE',  ( -0.7071067811865486830, 0.7071067811865464625, 0.000000000000000000 ) ) ;
#62226=VECTOR ( 'NONE', #3176, 1000.000000000000000 ) ;
#62227=CARTESIAN_POINT ( 'NONE',  ( 34.92499999999998295, 1.701930566820966773, 4.500000000000000888 ) ) ;
#62228=AXIS2_PLACEMENT_3D ( 'NONE', #9600, #8850, #111049 ) ;
#62229=CARTESIAN_POINT ( 'NONE',  ( 21.18398860626899349, 28.73617430169802134, 5.000000000000000000 ) ) ;
#62230=CARTESIAN_POINT ( 'NONE',  ( -0.1839886062690032631, 28.73617430169787568, 5.000000000000000000 ) ) ;
#62231=CARTESIAN_POINT ( 'NONE',  ( 24.48921356237309510, -27.52281430457072631, 5.000000000000000000 ) ) ;
#62232=ADVANCED_FACE ( 'NONE', ( #64409 ), #62290, .F. ) ;
#62234=CARTESIAN_POINT ( 'NONE',  ( -27.70710678118634718, -6.740707523384212863, 5.000000000000000000 ) ) ;
#62235=FACE_OUTER_BOUND ( 'NONE', #94147, .T. ) ;
#62236=ORIENTED_EDGE ( 'NONE', *, *, #37426, .T. ) ;
#62237=DIRECTION ( 'NONE',  ( -0.000000000000000000, 0.3543493200069153248, 0.9351131265310292928 ) ) ;
#62238=CARTESIAN_POINT ( 'NONE',  ( -6.489213562373093325, -27.52281430457059841, 5.000000000000000000 ) ) ;
#62239=ORIENTED_EDGE ( 'NONE', *, *, #93, .T. ) ;
#62240=LINE ( 'NONE', #40493, #78448 ) ;
#62241=LINE ( 'NONE', #7082, #122892 ) ;
#62242=ORIENTED_EDGE ( 'NONE', *, *, #80724, .T. ) ;
#62243=EDGE_CURVE ( 'NONE', #23479, #72219, #19476, .T. ) ;
#62244=CARTESIAN_POINT ( 'NONE',  ( -5.999999999999956479, 4.384688058510558761, -7.090945410444697394 ) ) ;
#62245=EDGE_CURVE ( 'NONE', #20046, #36553, #140530, .T. ) ;
#62247=DIRECTION ( 'NONE',  ( 1.000000000000000000, 0.000000000000000000, 0.000000000000000000 ) ) ;
#62248=VERTEX_POINT ( 'NONE', #6403 ) ;
#62249=DIRECTION ( 'NONE',  ( 0.000000000000000000, -0.3543493200069153248, -0.9351131265310291818 ) ) ;
#62250=EDGE_CURVE ( 'NONE', #126389, #74597, #41222, .T. ) ;
#62252=PLANE ( 'NONE',  #129508 ) ;
#62253=DIRECTION ( 'NONE',  ( 0.7071067811865487940, 0.7071067811865463515, 0.000000000000000000 ) ) ;
#62254=CARTESIAN_POINT ( 'NONE',  ( -10.49999999999991296, -17.94781430457065241, 5.000000000000000000 ) ) ;
#62259=CARTESIAN_POINT ( 'NONE',  ( -60.48921356237309510, -27.52281430457097500, 5.000000000000000000 ) ) ;
#62260=CARTESIAN_POINT ( 'NONE',  ( -34.47516574401891631, 16.49051761211544331, 4.998110765256835286 ) ) ;
#62261=PLANE ( 'NONE',  #61798 ) ;
#62262=EDGE_LOOP ( 'NONE', ( #137193, #72509, #64676, #3741 ) ) ;
#62263=EDGE_CURVE ( 'NONE', #105769, #64475, #20166, .T. ) ;
#62264=ORIENTED_EDGE ( 'NONE', *, *, #86758, .F. ) ;
#62266=EDGE_CURVE ( 'NONE', #71647, #94488, #9268, .T. ) ;
#62267=CARTESIAN_POINT ( 'NONE',  ( -33.48921356237309510, -27.52281430457078670, 5.000000000000000000 ) ) ;
#62268=EDGE_LOOP ( 'NONE', ( #116376, #93201, #115697, #18596 ) ) ;
#62269=VECTOR ( 'NONE', #107997, 999.9999999999998863 ) ;
#62271=DIRECTION ( 'NONE',  ( -0.7071067811865486830, -0.7071067811865464625, 0.000000000000000000 ) ) ;
#62272=EDGE_LOOP ( 'NONE', ( #134201, #101871, #108812, #130846, #5367 ) ) ;
#62274=VECTOR ( 'NONE', #142464, 1000.000000000000000 ) ;
#62276=LINE ( 'NONE', #17319, #111102 ) ;
#62277=LINE ( 'NONE', #52095, #67293 ) ;
#62279=CARTESIAN_POINT ( 'NONE',  ( 14.99999999999990230, 12.25461709320622639, -10.07315571508693708 ) ) ;
#62281=EDGE_CURVE ( 'NONE', #131664, #130620, #83322, .T. ) ;
#62283=CARTESIAN_POINT ( 'NONE',  ( -32.99999999999976552, 19.55218569542897100, 5.000000000000000000 ) ) ;
#62284=VECTOR ( 'NONE', #75917, 1000.000000000000000 ) ;
#62285=PLANE ( 'NONE',  #29063 ) ;
#62286=CARTESIAN_POINT ( 'NONE',  ( -47.99451991528749062, 28.92564299267971251, 4.000000000000000000 ) ) ;
#62287=FACE_OUTER_BOUND ( 'NONE', #98716, .T. ) ;
#62288=AXIS2_PLACEMENT_3D ( 'NONE', #24074, #3017, #13161 ) ;
#62289=LINE ( 'NONE', #120741, #137844 ) ;
#62290=PLANE ( 'NONE',  #83940 ) ;
#62291=ORIENTED_EDGE ( 'NONE', *, *, #16957, .F. ) ;
#62292=ORIENTED_EDGE ( 'NONE', *, *, #66457, .F. ) ;
#62294=VERTEX_POINT ( 'NONE', #117337 ) ;
#62295=VECTOR ( 'NONE', #7274, 1000.000000000000000 ) ;
#62296=AXIS2_PLACEMENT_3D ( 'NONE', #34626, #122316, #123073 ) ;
#62298=ORIENTED_EDGE ( 'NONE', *, *, #99072, .F. ) ;
#62299=CARTESIAN_POINT ( 'NONE',  ( 19.49999999999986500, -20.56887692260759337, 4.000000000000000000 ) ) ;
#62302=VECTOR ( 'NONE', #12670, 1000.000000000000000 ) ;
#62304=EDGE_LOOP ( 'NONE', ( #11963, #7702, #113164, #10194 ) ) ;
#62305=PLANE ( 'NONE',  #60558 ) ;
#62306=EDGE_LOOP ( 'NONE', ( #92647, #24339, #44430, #36657 ) ) ;
#62307=LINE ( 'NONE', #41237, #140274 ) ;
#62308=CARTESIAN_POINT ( 'NONE',  ( 66.48921356237309510, -27.52281430457101763, 5.000000000000000000 ) ) ;
#62312=VECTOR ( 'NONE', #101820, 1000.000000000000000 ) ;
#62313=VECTOR ( 'NONE', #19257, 999.9999999999998863 ) ;
#62314=ORIENTED_EDGE ( 'NONE', *, *, #81284, .T. ) ;
#62315=ORIENTED_EDGE ( 'NONE', *, *, #37954, .T. ) ;
#62317=VERTEX_POINT ( 'NONE', #132565 ) ;
#62318=LINE ( 'NONE', #49315, #111597 ) ;
#62319=EDGE_CURVE ( 'NONE', #115069, #141369, #133263, .T. ) ;
#62320=LINE ( 'NONE', #5018, #24571 ) ;
#62322=AXIS2_PLACEMENT_3D ( 'NONE', #27285, #71538, #93978 ) ;
#62323=VECTOR ( 'NONE', #20235, 1000.000000000000000 ) ;
#62324=DIRECTION ( 'NONE',  ( -0.000000000000000000, 0.000000000000000000, 1.000000000000000000 ) ) ;
#62325=EDGE_CURVE ( 'NONE', #58304, #56879, #57145, .T. ) ;
#62326=EDGE_CURVE ( 'NONE', #87749, #38833, #43382, .T. ) ;
#62328=ORIENTED_EDGE ( 'NONE', *, *, #85716, .F. ) ;
#62329=EDGE_LOOP ( 'NONE', ( #56283, #61127, #89932, #104068 ) ) ;
#62331=EDGE_CURVE ( 'NONE', #93380, #77093, #23771, .T. ) ;
#62332=ORIENTED_EDGE ( 'NONE', *, *, #50078, .F. ) ;
#62333=ORIENTED_EDGE ( 'NONE', *, *, #122586, .T. ) ;
#62334=AXIS2_PLACEMENT_3D ( 'NONE', #41514, #53094, #74904 ) ;
#62335=ADVANCED_FACE ( 'NONE', ( #42688 ), #110040, .F. ) ;
#62336=EDGE_CURVE ( 'NONE', #108896, #48371, #78885, .T. ) ;
#62338=LINE ( 'NONE', #40580, #107392 ) ;
#62339=VERTEX_POINT ( 'NONE', #133953 ) ;
#62340=LINE ( 'NONE', #81968, #120059 ) ;
#62341=CARTESIAN_POINT ( 'NONE',  ( 34.92499999999998295, 22.22500000000000142, 4.500000000000000888 ) ) ;
#62342=DIRECTION ( 'NONE',  ( 0.3543493200069162685, -0.000000000000000000, -0.9351131265310288487 ) ) ;
#62343=CARTESIAN_POINT ( 'NONE',  ( 66.48921356237309510, -27.52281430457101763, 5.000000000000000000 ) ) ;
#62344=VERTEX_POINT ( 'NONE', #131820 ) ;
#62345=ADVANCED_FACE ( 'NONE', ( #77464 ), #98464, .F. ) ;
#62346=CARTESIAN_POINT ( 'NONE',  ( 5.207106781186508826, -11.24070752338417556, 5.000000000000000000 ) ) ;
#62347=FACE_BOUND ( 'NONE', #43113, .T. ) ;
#62348=ORIENTED_EDGE ( 'NONE', *, *, #112748, .F. ) ;
#62349=CARTESIAN_POINT ( 'NONE',  ( 39.48921356237310221, -27.52281430457082934, 5.000000000000000000 ) ) ;
#62350=CARTESIAN_POINT ( 'NONE',  ( 66.18398860626901126, 28.73617430169833753, 5.000000000000000000 ) ) ;
#62351=CARTESIAN_POINT ( 'NONE',  ( 27.70710678118635428, 2.259292476615694323, 5.000000000000000000 ) ) ;
#62352=VERTEX_POINT ( 'NONE', #99149 ) ;
#62355=ORIENTED_EDGE ( 'NONE', *, *, #13852, .F. ) ;
#62356=EDGE_CURVE ( 'NONE', #39995, #100143, #28183, .T. ) ;
#62359=CARTESIAN_POINT ( 'NONE',  ( 34.92499999999998295, 10.70193056682087906, 4.500000000000000888 ) ) ;
#62363=PLANE ( 'NONE',  #13437 ) ;
#62364=CARTESIAN_POINT ( 'NONE',  ( -29.57672154193627989, 11.25929247661560240, 17.85071094206591269 ) ) ;
#62365=DIRECTION ( 'NONE',  ( 0.7071067811865487940, 0.7071067811865463515, 0.000000000000000000 ) ) ;
#62366=CARTESIAN_POINT ( 'NONE',  ( 6.183988606268994381, 28.73617430169791476, 5.000000000000000000 ) ) ;
#62367=LINE ( 'NONE', #7944, #19291 ) ;
#62368=VERTEX_POINT ( 'NONE', #89729 ) ;
#62369=EDGE_CURVE ( 'NONE', #106778, #59322, #121627, .T. ) ;
#62370=VERTEX_POINT ( 'NONE', #22296 ) ;
#62373=ORIENTED_EDGE ( 'NONE', *, *, #130750, .T. ) ;
#62374=PLANE ( 'NONE',  #107403 ) ;
#62375=VECTOR ( 'NONE', #86817, 1000.000000000000000 ) ;
#62376=VERTEX_POINT ( 'NONE', #56447 ) ;
#62377=CIRCLE ( 'NONE', #117882, 0.5000000000000004441 ) ;
#62378=EDGE_CURVE ( 'NONE', #76266, #24327, #67282, .T. ) ;
#62379=VECTOR ( 'NONE', #36135, 1000.000000000000000 ) ;
#62380=ORIENTED_EDGE ( 'NONE', *, *, #91620, .T. ) ;
#62381=DIRECTION ( 'NONE',  ( 0.7071067811865487940, 0.7071067811865463515, 0.000000000000000000 ) ) ;
#62382=DIRECTION ( 'NONE',  ( 0.7071067811865487940, -0.7071067811865463515, 0.000000000000000000 ) ) ;
#62383=ORIENTED_EDGE ( 'NONE', *, *, #22971, .F. ) ;
#62385=VECTOR ( 'NONE', #21594, 1000.000000000000227 ) ;
#62388=CARTESIAN_POINT ( 'NONE',  ( -24.18398860626899705, 28.73617430169804265, 5.000000000000000000 ) ) ;
#62389=CARTESIAN_POINT ( 'NONE',  ( 30.18398860626900060, 28.73617430169808173, 5.000000000000000000 ) ) ;
#62393=CARTESIAN_POINT ( 'NONE',  ( -32.99999999999976552, 4.552185695429122880, 5.000000000000000000 ) ) ;
#62394=ADVANCED_FACE ( 'NONE', ( #110734 ), #11418, .T. ) ;
#62395=CARTESIAN_POINT ( 'NONE',  ( -29.99999999999979039, 15.45873954670182115, -0.03131636524287412238 ) ) ;
#62396=ORIENTED_EDGE ( 'NONE', *, *, #26127, .F. ) ;
#62398=LINE ( 'NONE', #64518, #17166 ) ;
#62399=VERTEX_POINT ( 'NONE', #563 ) ;
#62400=VECTOR ( 'NONE', #8509, 999.9999999999998863 ) ;
#62401=CARTESIAN_POINT ( 'NONE',  ( 27.18398860626900060, 28.73617430169806042, 5.000000000000000000 ) ) ;
#62403=FACE_OUTER_BOUND ( 'NONE', #142625, .T. ) ;
#62404=DIRECTION ( 'NONE',  ( -0.000000000000000000, 0.3543493200069153248, 0.9351131265310292928 ) ) ;
#62405=VERTEX_POINT ( 'NONE', #44855 ) ;
#62408=CARTESIAN_POINT ( 'NONE',  ( 12.48921356237309155, -27.52281430457064104, 5.000000000000000000 ) ) ;
#62409=DIRECTION ( 'NONE',  ( -0.6830127018922180770, -0.6830127018922204085, -0.2588190451025213501 ) ) ;
#62410=ORIENTED_EDGE ( 'NONE', *, *, #70626, .T. ) ;
#62411=CARTESIAN_POINT ( 'NONE',  ( 34.92499999999998295, -4.487538124160487030, 4.000000000000000000 ) ) ;
#62413=CARTESIAN_POINT ( 'NONE',  ( -22.82816939922337340, -2.240707523384255939, 4.000000000000000000 ) ) ;
#62416=VECTOR ( 'NONE', #71888, 1000.000000000000000 ) ;
#62418=VERTEX_POINT ( 'NONE', #100622 ) ;
#62419=ADVANCED_FACE ( 'NONE', ( #10024 ), #20888, .F. ) ;
#62420=FACE_OUTER_BOUND ( 'NONE', #65607, .T. ) ;
#62422=PLANE ( 'NONE',  #18256 ) ;
#62423=VERTEX_POINT ( 'NONE', #111480 ) ;
#62424=DIRECTION ( 'NONE',  ( -0.7071067811865487940, 0.7071067811865463515, 0.000000000000000000 ) ) ;
#62425=CARTESIAN_POINT ( 'NONE',  ( -0.005480084712502889671, 28.92564299267938210, 4.000000000000000000 ) ) ;
#62427=DIRECTION ( 'NONE',  ( -0.000000000000000000, 0.3543493200069153248, 0.9351131265310292928 ) ) ;
#62428=CARTESIAN_POINT ( 'NONE',  ( -42.29974487139158157, -27.71228299555235708, 4.000000000000000000 ) ) ;
#62429=LINE ( 'NONE', #106587, #25752 ) ;
#62431=CARTESIAN_POINT ( 'NONE',  ( 19.05000000000000071, 3.174999999999997158, 4.000000000000000000 ) ) ;
#62432=FACE_OUTER_BOUND ( 'NONE', #15062, .T. ) ;
#62433=VECTOR ( 'NONE', #136938, 1000.000000000000227 ) ;
#62434=FACE_OUTER_BOUND ( 'NONE', #9000, .T. ) ;
#62435=DIRECTION ( 'NONE',  ( -0.7071067811865487940, 0.7071067811865463515, -0.000000000000000000 ) ) ;
#62437=ORIENTED_EDGE ( 'NONE', *, *, #134281, .F. ) ;
#62438=ADVANCED_FACE ( 'NONE', ( #36767 ), #102765, .F. ) ;
#62439=ORIENTED_EDGE ( 'NONE', *, *, #20299, .T. ) ;
#62440=VERTEX_POINT ( 'NONE', #25177 ) ;
#62443=EDGE_LOOP ( 'NONE', ( #91028, #77925, #45923, #113521 ) ) ;
#62444=VERTEX_POINT ( 'NONE', #24471 ) ;
#62445=EDGE_LOOP ( 'NONE', ( #25471, #9252, #133656, #121846 ) ) ;
#62446=DIRECTION ( 'NONE',  ( -0.000000000000000000, -0.000000000000000000, 1.000000000000000000 ) ) ;
#62447=DIRECTION ( 'NONE',  ( 0.000000000000000000, 1.000000000000000000, 0.000000000000000000 ) ) ;
#62448=ORIENTED_EDGE ( 'NONE', *, *, #93232, .F. ) ;
#62450=CARTESIAN_POINT ( 'NONE',  ( -21.18398860626899349, 28.73617430169802134, 5.000000000000000000 ) ) ;
#62451=CARTESIAN_POINT ( 'NONE',  ( 0.000000000000000000, 0.000000000000000000, 5.000000000000000000 ) ) ;
#62452=DIRECTION ( 'NONE',  ( -0.000000000000000000, 0.3543493200069153248, 0.9351131265310292928 ) ) ;
#62455=EDGE_CURVE ( 'NONE', #42067, #126713, #90450, .T. ) ;
#62456=LINE ( 'NONE', #40697, #116366 ) ;
#62460=DIRECTION ( 'NONE',  ( -0.7071067811865486830, 0.7071067811865464625, 0.000000000000000000 ) ) ;
#62461=DIRECTION ( 'NONE',  ( 0.000000000000000000, 1.000000000000000000, 0.000000000000000000 ) ) ;
#62462=EDGE_LOOP ( 'NONE', ( #40512, #33407, #140248, #38857 ) ) ;
#62463=ORIENTED_EDGE ( 'NONE', *, *, #18487, .F. ) ;
#62465=ORIENTED_EDGE ( 'NONE', *, *, #135610, .F. ) ;
#62466=CYLINDRICAL_SURFACE ( 'NONE', #29781, 0.5000000000000004441 ) ;
#62467=CARTESIAN_POINT ( 'NONE',  ( -30.18398860626900060, 28.73617430169808173, 5.000000000000000000 ) ) ;
#62468=DIRECTION ( 'NONE',  ( 0.7071067811865487940, 0.7071067811865463515, 0.000000000000000000 ) ) ;
#62469=FACE_OUTER_BOUND ( 'NONE', #70410, .T. ) ;
#62471=CARTESIAN_POINT ( 'NONE',  ( 32.14818355038125475, 17.25929247661554200, 8.802941693769275489 ) ) ;
#62473=VERTEX_POINT ( 'NONE', #26617 ) ;
#62474=CARTESIAN_POINT ( 'NONE',  ( 27.48921356237309155, -27.52281430457074762, 5.000000000000000000 ) ) ;
#62476=DIRECTION ( 'NONE',  ( -0.000000000000000000, 0.3543493200069153248, 0.9351131265310292928 ) ) ;
#62477=VECTOR ( 'NONE', #32787, 1000.000000000000000 ) ;
#62478=VECTOR ( 'NONE', #20818, 1000.000000000000000 ) ;
#62481=VECTOR ( 'NONE', #130837, 1000.000000000000227 ) ;
#62482=DIRECTION ( 'NONE',  ( -0.3543493200069162685, -0.000000000000000000, -0.9351131265310288487 ) ) ;
#62483=EDGE_LOOP ( 'NONE', ( #92531, #68041, #82078, #21957 ) ) ;
#62486=DIRECTION ( 'NONE',  ( 0.7071067811865486830, -0.7071067811865464625, -0.000000000000000000 ) ) ;
#62487=CARTESIAN_POINT ( 'NONE',  ( -10.17183060077639212, 21.75929247661549581, 4.000000000000000000 ) ) ;
#62488=DIRECTION ( 'NONE',  ( 1.000000000000000000, 0.000000000000000000, 0.000000000000000000 ) ) ;
#62491=( BOUNDED_CURVE ( )  B_SPLINE_CURVE ( 3, ( #111871, #12535, #56813, #1631 ),
 .UNSPECIFIED., .F., .T. ) 
 B_SPLINE_CURVE_WITH_KNOTS ( ( 4, 4 ),
 ( 1.901594255663624056, 1.933014472006554740 ),
 .UNSPECIFIED. ) 
 CURVE ( )  GEOMETRIC_REPRESENTATION_ITEM ( )  RATIONAL_B_SPLINE_CURVE ( ( 1.000000000000000000, 0.9999177325257868620, 0.9999177325257868620, 1.000000000000000000 ) ) 
 REPRESENTATION_ITEM ( '' )  );
#62492=ADVANCED_FACE ( 'NONE', ( #25906 ), #38219, .F. ) ;
#62493=AXIS2_PLACEMENT_3D ( 'NONE', #84349, #62578, #106761 ) ;
#62496=ORIENTED_EDGE ( 'NONE', *, *, #34402, .F. ) ;
#62498=PLANE ( 'NONE',  #74368 ) ;
#62499=DIRECTION ( 'NONE',  ( 0.6830127018922181881, 0.6830127018922202975, -0.2588190451025214056 ) ) ;
#62500=EDGE_CURVE ( 'NONE', #4447, #136109, #104141, .T. ) ;
#62501=VERTEX_POINT ( 'NONE', #126619 ) ;
#62502=ORIENTED_EDGE ( 'NONE', *, *, #102313, .T. ) ;
#62505=ORIENTED_EDGE ( 'NONE', *, *, #19322, .T. ) ;
#62506=EDGE_CURVE ( 'NONE', #56761, #100010, #79634, .T. ) ;
#62507=VECTOR ( 'NONE', #49821, 1000.000000000000000 ) ;
#62508=CARTESIAN_POINT ( 'NONE',  ( -34.42500000000001137, 1.541399257802000822, 5.000000000000000000 ) ) ;
#62509=LINE ( 'NONE', #71246, #104361 ) ;
#62511=CARTESIAN_POINT ( 'NONE',  ( -36.29974487139159578, -27.71228299555231445, 4.000000000000000000 ) ) ;
#62512=ADVANCED_FACE ( 'NONE', ( #2708 ), #47007, .F. ) ;
#62513=VECTOR ( 'NONE', #108405, 1000.000000000000000 ) ;
#62514=VECTOR ( 'NONE', #34814, 1000.000000000000227 ) ;
#62516=ADVANCED_FACE ( 'NONE', ( #129483 ), #128094, .F. ) ;
#62517=FACE_BOUND ( 'NONE', #137669, .T. ) ;
#62518=EDGE_CURVE ( 'NONE', #80963, #124390, #140369, .T. ) ;
#62519=CARTESIAN_POINT ( 'NONE',  ( -71.99451991528749772, 28.92564299267988304, 4.000000000000000000 ) ) ;
#62520=AXIS2_PLACEMENT_3D ( 'NONE', #15936, #48623, #115248 ) ;
#62522=DIRECTION ( 'NONE',  ( -0.000000000000000000, -1.000000000000000000, -0.000000000000000000 ) ) ;
#62523=ORIENTED_EDGE ( 'NONE', *, *, #47251, .F. ) ;
#62526=ORIENTED_EDGE ( 'NONE', *, *, #111409, .F. ) ;
#62527=FACE_OUTER_BOUND ( 'NONE', #73866, .T. ) ;
#62529=ORIENTED_EDGE ( 'NONE', *, *, #93760, .T. ) ;
#62532=FACE_OUTER_BOUND ( 'NONE', #69697, .T. ) ;
#62533=CARTESIAN_POINT ( 'NONE',  ( -19.49999999999985079, -4.912538124160707120, 4.000000000000000000 ) ) ;
#62535=DIRECTION ( 'NONE',  ( -0.7071067811865486830, -0.7071067811865464625, 0.000000000000000000 ) ) ;
#62536=AXIS2_PLACEMENT_3D ( 'NONE', #83673, #73488, #128571 ) ;
#62538=CARTESIAN_POINT ( 'NONE',  ( 5.816011393731002066, 28.73617430169783304, 5.000000000000000000 ) ) ;
#62539=CARTESIAN_POINT ( 'NONE',  ( -14.24139925780194105, 21.72500000000000142, 5.000000000000000000 ) ) ;
#62540=LINE ( 'NONE', #59690, #72528 ) ;
#62541=PLANE ( 'NONE',  #11503 ) ;
#62542=ORIENTED_EDGE ( 'NONE', *, *, #130967, .T. ) ;
#62543=EDGE_CURVE ( 'NONE', #106767, #109446, #8388, .T. ) ;
#62545=ORIENTED_EDGE ( 'NONE', *, *, #2570, .F. ) ;
#62547=PLANE ( 'NONE',  #30479 ) ;
#62550=ORIENTED_EDGE ( 'NONE', *, *, #27860, .T. ) ;
#62551=DIRECTION ( 'NONE',  ( -0.6830127018922181881, 0.6830127018922202975, -0.2588190451025214056 ) ) ;
#62553=ORIENTED_EDGE ( 'NONE', *, *, #126744, .T. ) ;
#62554=PLANE ( 'NONE',  #99551 ) ;
#62555=VECTOR ( 'NONE', #104843, 1000.000000000000227 ) ;
#62557=DIRECTION ( 'NONE',  ( 0.3543493200069162685, -0.000000000000000000, -0.9351131265310288487 ) ) ;
#62558=ORIENTED_EDGE ( 'NONE', *, *, #38155, .F. ) ;
#62559=CARTESIAN_POINT ( 'NONE',  ( -34.92500000000001137, 22.22500000000000142, 4.000000000000000000 ) ) ;
#62560=DIRECTION ( 'NONE',  ( 0.7071067811865487940, 0.7071067811865463515, 0.000000000000000000 ) ) ;
#62562=DIRECTION ( 'NONE',  ( -0.7071067811865486830, -0.7071067811865464625, 0.000000000000000000 ) ) ;
#62563=CARTESIAN_POINT ( 'NONE',  ( 0.000000000000000000, 0.000000000000000000, 5.000000000000000000 ) ) ;
#62564=ORIENTED_EDGE ( 'NONE', *, *, #91941, .T. ) ;
#62566=ORIENTED_EDGE ( 'NONE', *, *, #91434, .T. ) ;
#62567=PLANE ( 'NONE',  #28780 ) ;
#62568=DIRECTION ( 'NONE',  ( -0.000000000000000000, 0.000000000000000000, 1.000000000000000000 ) ) ;
#62569=DIRECTION ( 'NONE',  ( 0.7071067811865487940, 0.7071067811865463515, 0.000000000000000000 ) ) ;
#62573=CARTESIAN_POINT ( 'NONE',  ( 34.92499999999998295, 12.85612307739228477, 4.000000000000000000 ) ) ;
#62574=ORIENTED_EDGE ( 'NONE', *, *, #2969, .T. ) ;
#62575=AXIS2_PLACEMENT_3D ( 'NONE', #13659, #36174, #113717 ) ;
#62576=VECTOR ( 'NONE', #26208, 1000.000000000000000 ) ;
#62577=VECTOR ( 'NONE', #39950, 999.9999999999998863 ) ;
#62578=DIRECTION ( 'NONE',  ( 0.6830127018922181881, 0.6830127018922202975, -0.2588190451025214056 ) ) ;
#62580=LINE ( 'NONE', #30670, #12230 ) ;
#62581=VECTOR ( 'NONE', #15755, 1000.000000000000000 ) ;
#62582=CARTESIAN_POINT ( 'NONE',  ( -20.99999999999985079, 20.96639925780204905, 5.000000000000000000 ) ) ;
#62583=EDGE_LOOP ( 'NONE', ( #59550, #110665, #52480, #6871 ) ) ;
#62584=EDGE_CURVE ( 'NONE', #61664, #74056, #116481, .T. ) ;
#62585=ORIENTED_EDGE ( 'NONE', *, *, #96012, .T. ) ;
#62587=VECTOR ( 'NONE', #68524, 1000.000000000000227 ) ;
#62590=CARTESIAN_POINT ( 'NONE',  ( -8.816011393731004731, 28.73617430169781173, 5.000000000000000000 ) ) ;
#62591=FACE_OUTER_BOUND ( 'NONE', #57008, .T. ) ;
#62592=PLANE ( 'NONE',  #111594 ) ;
#62593=ORIENTED_EDGE ( 'NONE', *, *, #99858, .F. ) ;
#62594=LINE ( 'NONE', #106779, #55791 ) ;
#62597=VECTOR ( 'NONE', #59399, 1000.000000000000227 ) ;
#62601=VECTOR ( 'NONE', #124870, 1000.000000000000000 ) ;
#62602=ORIENTED_EDGE ( 'NONE', *, *, #6687, .T. ) ;
#62603=FACE_OUTER_BOUND ( 'NONE', #41662, .T. ) ;
#62604=AXIS2_PLACEMENT_3D ( 'NONE', #81261, #124738, #89261 ) ;
#62605=EDGE_CURVE ( 'NONE', #40303, #64278, #49829, .T. ) ;
#62606=ORIENTED_EDGE ( 'NONE', *, *, #37252, .F. ) ;
#62607=ADVANCED_FACE ( 'NONE', ( #73693 ), #105577, .F. ) ;
#62608=VECTOR ( 'NONE', #20689, 1000.000000000000000 ) ;
#62609=ORIENTED_EDGE ( 'NONE', *, *, #58312, .F. ) ;
#62610=LINE ( 'NONE', #7479, #52388 ) ;
#62611=VECTOR ( 'NONE', #27990, 1000.000000000000000 ) ;
#62613=CARTESIAN_POINT ( 'NONE',  ( 3.005480084712505828, 28.92564299267936079, 4.000000000000000000 ) ) ;
#62615=EDGE_CURVE ( 'NONE', #88778, #95164, #138238, .T. ) ;
#62616=CARTESIAN_POINT ( 'NONE',  ( -16.49999999999988276, 8.319652575858368593, -8.582050562765862978 ) ) ;
#62617=CARTESIAN_POINT ( 'NONE',  ( -29.20710678118634362, 12.75929247661559351, 5.000000000000000000 ) ) ;
#62618=VECTOR ( 'NONE', #84675, 1000.000000000000000 ) ;
#62620=EDGE_CURVE ( 'NONE', #105795, #100461, #30177, .T. ) ;
#62621=LINE ( 'NONE', #60496, #102256 ) ;
#62622=CARTESIAN_POINT ( 'NONE',  ( 14.51078643762690490, -27.52281430457045275, 5.000000000000000000 ) ) ;
#62624=CARTESIAN_POINT ( 'NONE',  ( 66.48921356237309510, -27.52281430457101763, 5.000000000000000000 ) ) ;
#62628=DIRECTION ( 'NONE',  ( -0.7071067811865486830, -0.7071067811865464625, 0.000000000000000000 ) ) ;
#62629=VECTOR ( 'NONE', #87290, 999.9999999999998863 ) ;
#62630=EDGE_LOOP ( 'NONE', ( #77300, #26103, #55882, #120929 ) ) ;
#62631=EDGE_LOOP ( 'NONE', ( #14500, #9297, #110345, #83210 ) ) ;
#62633=CARTESIAN_POINT ( 'NONE',  ( 32.29289321881324071, -12.74070752338415069, 5.000000000000000000 ) ) ;
#62634=CARTESIAN_POINT ( 'NONE',  ( 22.82816939922337340, 21.75929247661548516, 4.000000000000000000 ) ) ;
#62635=AXIS2_PLACEMENT_3D ( 'NONE', #7856, #127516, #94158 ) ;
#62636=DIRECTION ( 'NONE',  ( -0.7071067811865486830, 0.7071067811865464625, 0.000000000000000000 ) ) ;
#62637=EDGE_LOOP ( 'NONE', ( #21663, #80433, #19734, #31090, #12927 ) ) ;
#62643=ORIENTED_EDGE ( 'NONE', *, *, #86110, .F. ) ;
#62645=CARTESIAN_POINT ( 'NONE',  ( 36.48921356237310221, -27.52281430457080802, 5.000000000000000000 ) ) ;
#62646=CARTESIAN_POINT ( 'NONE',  ( -31.49999999999978684, 8.319652575858354382, -8.582050562765896728 ) ) ;
#62647=CARTESIAN_POINT ( 'NONE',  ( -3.489213562373097322, -27.52281430457057709, 5.000000000000000000 ) ) ;
#62649=DIRECTION ( 'NONE',  ( 0.7071067811865487940, 0.7071067811865463515, 0.000000000000000000 ) ) ;
#62650=DIRECTION ( 'NONE',  ( -0.7071067811865486830, -0.7071067811865464625, 0.000000000000000000 ) ) ;
#62653=CARTESIAN_POINT ( 'NONE',  ( 21.29974487139158512, -27.71228299555221142, 4.000000000000000000 ) ) ;
#62654=DIRECTION ( 'NONE',  ( 0.7071067811865487940, 0.7071067811865463515, 0.000000000000000000 ) ) ;
#62655=CARTESIAN_POINT ( 'NONE',  ( 27.29974487139158512, -27.71228299555225405, 4.000000000000000000 ) ) ;
#62657=LINE ( 'NONE', #139532, #53024 ) ;
#62659=ORIENTED_EDGE ( 'NONE', *, *, #102259, .T. ) ;
#62660=EDGE_CURVE ( 'NONE', #28277, #57736, #131654, .T. ) ;
#62661=ORIENTED_EDGE ( 'NONE', *, *, #106155, .T. ) ;
#62664=EDGE_CURVE ( 'NONE', #36664, #88273, #73950, .T. ) ;
#62665=DIRECTION ( 'NONE',  ( 0.6830127018922180770, -0.6830127018922204085, -0.2588190451025213501 ) ) ;
#62666=LINE ( 'NONE', #52477, #75534 ) ;
#62668=ORIENTED_EDGE ( 'NONE', *, *, #85923, .T. ) ;
#62669=ORIENTED_EDGE ( 'NONE', *, *, #95824, .T. ) ;
#62670=DIRECTION ( 'NONE',  ( 0.7071067811865487940, -0.7071067811865463515, 0.000000000000000000 ) ) ;
#62671=CARTESIAN_POINT ( 'NONE',  ( -23.99999999999983658, 18.08204922493371214, 0.9627537363045436392 ) ) ;
#62673=ORIENTED_EDGE ( 'NONE', *, *, #136031, .F. ) ;
#62675=EDGE_CURVE ( 'NONE', #84892, #111297, #89556, .T. ) ;
#62676=AXIS2_PLACEMENT_3D ( 'NONE', #127927, #72868, #103981 ) ;
#62677=ORIENTED_EDGE ( 'NONE', *, *, #79496, .F. ) ;
#62678=PLANE ( 'NONE',  #130069 ) ;
#62679=VERTEX_POINT ( 'NONE', #143230 ) ;
#62681=CIRCLE ( 'NONE', #110, 5.968999999999998529 ) ;
#62682=VECTOR ( 'NONE', #62798, 1000.000000000000000 ) ;
#62683=VECTOR ( 'NONE', #139065, 1000.000000000000000 ) ;
#62684=VECTOR ( 'NONE', #87364, 1000.000000000000000 ) ;
#62685=VECTOR ( 'NONE', #14913, 1000.000000000000000 ) ;
#62686=DIRECTION ( 'NONE',  ( 0.6830127018922181881, 0.6830127018922202975, -0.2588190451025214056 ) ) ;
#62687=EDGE_CURVE ( 'NONE', #63098, #61017, #43929, .T. ) ;
#62688=FACE_BOUND ( 'NONE', #7199, .T. ) ;
#62689=ADVANCED_FACE ( 'NONE', ( #98309 ), #11985, .F. ) ;
#62690=DIRECTION ( 'NONE',  ( 1.000000000000000000, 0.000000000000000000, 0.000000000000000000 ) ) ;
#62691=CARTESIAN_POINT ( 'NONE',  ( 0.000000000000000000, -21.72500000000000142, 4.500000000000000888 ) ) ;
#62692=AXIS2_PLACEMENT_3D ( 'NONE', #116638, #40524, #28215 ) ;
#62693=DIRECTION ( 'NONE',  ( -0.7071067811865487940, 0.7071067811865463515, 0.000000000000000000 ) ) ;
#62694=CARTESIAN_POINT ( 'NONE',  ( 0.1839886062690032631, 28.73617430169787568, 5.000000000000000000 ) ) ;
#62695=ORIENTED_EDGE ( 'NONE', *, *, #49638, .T. ) ;
#62698=EDGE_CURVE ( 'NONE', #39646, #109641, #9093, .T. ) ;
#62699=VERTEX_POINT ( 'NONE', #88150 ) ;
#62700=ORIENTED_EDGE ( 'NONE', *, *, #113244, .T. ) ;
#62702=ORIENTED_EDGE ( 'NONE', *, *, #108791, .F. ) ;
#62703=CARTESIAN_POINT ( 'NONE',  ( -34.42500000000001137, -22.22500000000000142, 5.000000000000000000 ) ) ;
#62704=LINE ( 'NONE', #27909, #242 ) ;
#62705=AXIS2_PLACEMENT_3D ( 'NONE', #128732, #130904, #9801 ) ;
#62706=DIRECTION ( 'NONE',  ( -0.3543493200069162685, -0.000000000000000000, -0.9351131265310288487 ) ) ;
#62707=EDGE_CURVE ( 'NONE', #100524, #81804, #88875, .T. ) ;
#62708=VECTOR ( 'NONE', #107910, 1000.000000000000000 ) ;
#62709=CARTESIAN_POINT ( 'NONE',  ( 45.29974487139158867, -27.71228299555237840, 4.000000000000000000 ) ) ;
#62710=DIRECTION ( 'NONE',  ( 0.7071067811865486830, -0.7071067811865464625, -0.000000000000000000 ) ) ;
#62711=VECTOR ( 'NONE', #49655, 1000.000000000000000 ) ;
#62712=CARTESIAN_POINT ( 'NONE',  ( 11.20710678118647152, -2.240707523384259492, 5.000000000000000000 ) ) ;
#62714=PLANE ( 'NONE',  #75169 ) ;
#62715=AXIS2_PLACEMENT_3D ( 'NONE', #13907, #14652, #89353 ) ;
#62716=CARTESIAN_POINT ( 'NONE',  ( 39.29974487139159578, -27.71228299555233576, 4.000000000000000000 ) ) ;
#62717=DIRECTION ( 'NONE',  ( 0.6830127018922181881, 0.6830127018922202975, -0.2588190451025214056 ) ) ;
#62718=EDGE_CURVE ( 'NONE', #13719, #124122, #132394, .T. ) ;
#62719=CARTESIAN_POINT ( 'NONE',  ( -34.49999999999976552, 0.4311230773921780335, 4.000000000000000000 ) ) ;
#62720=ORIENTED_EDGE ( 'NONE', *, *, #36611, .F. ) ;
#62722=DIRECTION ( 'NONE',  ( -0.000000000000000000, 0.3543493200069153248, 0.9351131265310292928 ) ) ;
#62723=DIRECTION ( 'NONE',  ( -0.7071067811865486830, 0.7071067811865464625, 0.000000000000000000 ) ) ;
#62724=EDGE_LOOP ( 'NONE', ( #40917, #62602, #2901, #34311 ) ) ;
#62726=AXIS2_PLACEMENT_3D ( 'NONE', #124270, #16184, #138012 ) ;
#62727=ORIENTED_EDGE ( 'NONE', *, *, #3778, .T. ) ;
#62728=ADVANCED_FACE ( 'NONE', ( #87436 ), #11251, .F. ) ;
#62730=ADVANCED_FACE ( 'NONE', ( #121464 ), #9851, .F. ) ;
#62732=DIRECTION ( 'NONE',  ( 0.7071067811865487940, 0.7071067811865463515, 0.000000000000000000 ) ) ;
#62733=EDGE_CURVE ( 'NONE', #42516, #138332, #124866, .T. ) ;
#62734=AXIS2_PLACEMENT_3D ( 'NONE', #3877, #37277, #126406 ) ;
#62737=ORIENTED_EDGE ( 'NONE', *, *, #52215, .T. ) ;
#62738=DIRECTION ( 'NONE',  ( -0.7071067811865487940, 0.7071067811865463515, 0.000000000000000000 ) ) ;
#62739=ORIENTED_EDGE ( 'NONE', *, *, #71853, .T. ) ;
#62740=FACE_OUTER_BOUND ( 'NONE', #133154, .T. ) ;
#62741=CYLINDRICAL_SURFACE ( 'NONE', #19740, 0.5000000000000004441 ) ;
#62742=CARTESIAN_POINT ( 'NONE',  ( 15.99507522778795909, -5.240707523384225297, 12.38332538355492218 ) ) ;
#62743=VERTEX_POINT ( 'NONE', #78690 ) ;
#62745=PLANE ( 'NONE',  #537 ) ;
#62746=VERTEX_POINT ( 'NONE', #64249 ) ;
#62747=DIRECTION ( 'NONE',  ( -0.6830127018922180770, -0.6830127018922204085, -0.2588190451025213501 ) ) ;
#62749=VERTEX_POINT ( 'NONE', #54121 ) ;
#62752=LINE ( 'NONE', #49018, #30973 ) ;
#62753=VECTOR ( 'NONE', #31708, 1000.000000000000000 ) ;
#62754=DIRECTION ( 'NONE',  ( -0.7071067811865487940, 0.7071067811865463515, 0.000000000000000000 ) ) ;
#62755=CARTESIAN_POINT ( 'NONE',  ( 62.99451991528749772, 28.92564299267982264, 4.000000000000000000 ) ) ;
#62756=LINE ( 'NONE', #106942, #107275 ) ;
#62757=CARTESIAN_POINT ( 'NONE',  ( -34.49999999999975842, -6.839392718269155402, -8.480912228396004338 ) ) ;
#62758=ORIENTED_EDGE ( 'NONE', *, *, #83919, .T. ) ;
#62759=CARTESIAN_POINT ( 'NONE',  ( -45.18398860626900415, 28.73617430169818832, 5.000000000000000000 ) ) ;
#62761=AXIS2_PLACEMENT_3D ( 'NONE', #52265, #97159, #141424 ) ;
#62762=LINE ( 'NONE', #106949, #44862 ) ;
#62764=CARTESIAN_POINT ( 'NONE',  ( -66.48921356237309510, -27.52281430457101763, 5.000000000000000000 ) ) ;
#62765=ORIENTED_EDGE ( 'NONE', *, *, #17777, .T. ) ;
#62766=PLANE ( 'NONE',  #66923 ) ;
#62768=ORIENTED_EDGE ( 'NONE', *, *, #105168, .F. ) ;
#62769=VERTEX_POINT ( 'NONE', #108412 ) ;
#62771=EDGE_LOOP ( 'NONE', ( #119194, #116691, #71340, #20007 ) ) ;
#62772=DIRECTION ( 'NONE',  ( -0.6830127018922181881, 0.6830127018922202975, -0.2588190451025214056 ) ) ;
#62773=FACE_OUTER_BOUND ( 'NONE', #10311, .T. ) ;
#62774=EDGE_CURVE ( 'NONE', #121745, #112217, #114849, .T. ) ;
#62776=DIRECTION ( 'NONE',  ( -0.000000000000000000, 0.000000000000000000, 1.000000000000000000 ) ) ;
#62780=PLANE ( 'NONE',  #127472 ) ;
#62781=VECTOR ( 'NONE', #45435, 999.9999999999998863 ) ;
#62782=AXIS2_PLACEMENT_3D ( 'NONE', #43408, #6616, #143422 ) ;
#62783=CARTESIAN_POINT ( 'NONE',  ( 34.92499999999998295, 3.856123077392373144, 4.000000000000000000 ) ) ;
#62784=DIRECTION ( 'NONE',  ( 0.6830127018922181881, 0.6830127018922202975, -0.2588190451025214056 ) ) ;
#62785=LINE ( 'NONE', #96087, #60635 ) ;
#62786=ORIENTED_EDGE ( 'NONE', *, *, #3323, .T. ) ;
#62787=CARTESIAN_POINT ( 'NONE',  ( -32.99451991528749062, 28.92564299267960948, 4.000000000000000000 ) ) ;
#62788=ORIENTED_EDGE ( 'NONE', *, *, #10334, .F. ) ;
#62790=AXIS2_PLACEMENT_3D ( 'NONE', #94494, #5337, #115504 ) ;
#62791=VECTOR ( 'NONE', #131962, 1000.000000000000000 ) ;
#62792=CARTESIAN_POINT ( 'NONE',  ( 16.63753812416085509, 22.22500000000000142, 4.000000000000000000 ) ) ;
#62794=CARTESIAN_POINT ( 'NONE',  ( 26.99451991528749417, 28.92564299267956685, 4.000000000000000000 ) ) ;
#62795=VERTEX_POINT ( 'NONE', #35213 ) ;
#62797=DIRECTION ( 'NONE',  ( 1.000000000000000000, 0.000000000000000000, 0.000000000000000000 ) ) ;
#62798=DIRECTION ( 'NONE',  ( -0.7071067811865486830, -0.7071067811865464625, 0.000000000000000000 ) ) ;
#62799=VERTEX_POINT ( 'NONE', #4620 ) ;
#62800=EDGE_CURVE ( 'NONE', #57534, #84656, #103976, .T. ) ;
#62801=PLANE ( 'NONE',  #139021 ) ;
#62802=CARTESIAN_POINT ( 'NONE',  ( -27.29974487139158512, -27.71228299555225405, 4.000000000000000000 ) ) ;
#62804=EDGE_CURVE ( 'NONE', #49877, #19355, #38055, .T. ) ;
#62806=LINE ( 'NONE', #106984, #42190 ) ;
#62808=LINE ( 'NONE', #84552, #82061 ) ;
#62810=LINE ( 'NONE', #109136, #23104 ) ;
#62813=EDGE_CURVE ( 'NONE', #46898, #15867, #12694, .T. ) ;
#62814=VECTOR ( 'NONE', #124373, 1000.000000000000000 ) ;
#62815=CARTESIAN_POINT ( 'NONE',  ( -48.48921356237309510, -27.52281430457089328, 5.000000000000000000 ) ) ;
#62816=LINE ( 'NONE', #60695, #94766 ) ;
#62817=LINE ( 'NONE', #84563, #75240 ) ;
#62818=CARTESIAN_POINT ( 'NONE',  ( -11.70025512860841133, -27.71228299555198049, 4.000000000000000000 ) ) ;
#62819=EDGE_LOOP ( 'NONE', ( #87800, #135293, #17786, #91579 ) ) ;
#62820=EDGE_CURVE ( 'NONE', #55970, #111086, #80850, .T. ) ;
#62821=VECTOR ( 'NONE', #4473, 1000.000000000000000 ) ;
#62823=EDGE_LOOP ( 'NONE', ( #142952, #51330, #130065, #42898 ) ) ;
#62824=VECTOR ( 'NONE', #59992, 1000.000000000000000 ) ;
#62826=AXIS2_PLACEMENT_3D ( 'NONE', #66632, #122410, #142065 ) ;
#62827=DIRECTION ( 'NONE',  ( 0.7071067811865487940, 0.7071067811865463515, 0.000000000000000000 ) ) ;
#62828=LINE ( 'NONE', #7687, #74802 ) ;
#62829=ORIENTED_EDGE ( 'NONE', *, *, #129670, .F. ) ;
#62830=ADVANCED_FACE ( 'NONE', ( #125040 ), #67858, .F. ) ;
#62831=VECTOR ( 'NONE', #103588, 1000.000000000000000 ) ;
#62833=DIRECTION ( 'NONE',  ( -0.7071067811865486830, -0.7071067811865464625, 0.000000000000000000 ) ) ;
#62834=AXIS2_PLACEMENT_3D ( 'NONE', #115313, #92890, #139287 ) ;
#62835=PLANE ( 'NONE',  #75309 ) ;
#62836=ORIENTED_EDGE ( 'NONE', *, *, #25016, .T. ) ;
#62838=CARTESIAN_POINT ( 'NONE',  ( 22.49999999999985079, -17.94781430457063820, 5.000000000000000000 ) ) ;
#62840=DIRECTION ( 'NONE',  ( -0.6830127018922180770, -0.6830127018922204085, -0.2588190451025213501 ) ) ;
#62842=EDGE_LOOP ( 'NONE', ( #6056, #120385, #22903, #86946 ) ) ;
#62844=VERTEX_POINT ( 'NONE', #136622 ) ;
#62845=LINE ( 'NONE', #130957, #89262 ) ;
#62846=EDGE_CURVE ( 'NONE', #58174, #3994, #69255, .T. ) ;
#62847=PLANE ( 'NONE',  #15591 ) ;
#62849=LINE ( 'NONE', #70872, #98677 ) ;
#62853=DIRECTION ( 'NONE',  ( 0.6830127018922180770, -0.6830127018922204085, -0.2588190451025213501 ) ) ;
#62854=ADVANCED_FACE ( 'NONE', ( #37334 ), #1786, .T. ) ;
#62855=EDGE_CURVE ( 'NONE', #102772, #129516, #113436, .T. ) ;
#62856=ORIENTED_EDGE ( 'NONE', *, *, #65433, .F. ) ;
#62857=PLANE ( 'NONE',  #127695 ) ;
#62858=VECTOR ( 'NONE', #31783, 1000.000000000000000 ) ;
#62860=CARTESIAN_POINT ( 'NONE',  ( -12.48921356237309155, -27.52281430457064104, 5.000000000000000000 ) ) ;
#62863=EDGE_LOOP ( 'NONE', ( #68759, #77887, #10321, #50474 ) ) ;
#62864=ORIENTED_EDGE ( 'NONE', *, *, #116977, .F. ) ;
#62865=EDGE_CURVE ( 'NONE', #135680, #30212, #112738, .T. ) ;
#62866=PLANE ( 'NONE',  #8289 ) ;
#62867=ADVANCED_FACE ( 'NONE', ( #91697 ), #69999, .F. ) ;
#62868=CARTESIAN_POINT ( 'NONE',  ( -26.99451991528749417, 28.92564299267956685, 4.000000000000000000 ) ) ;
#62869=CARTESIAN_POINT ( 'NONE',  ( 21.18398860626899349, 28.73617430169802134, 5.000000000000000000 ) ) ;
#62870=CARTESIAN_POINT ( 'NONE',  ( 8.999999999999932498, 14.87792677143809783, -11.06722581663437843 ) ) ;
#62872=AXIS2_PLACEMENT_3D ( 'NONE', #56952, #77971, #122152 ) ;
#62874=DIRECTION ( 'NONE',  ( 1.000000000000000000, 0.000000000000000000, 0.000000000000000000 ) ) ;
#62875=ORIENTED_EDGE ( 'NONE', *, *, #116127, .T. ) ;
#62876=ORIENTED_EDGE ( 'NONE', *, *, #113503, .T. ) ;
#62877=EDGE_LOOP ( 'NONE', ( #128436, #102690, #80511, #50070 ) ) ;
#62878=EDGE_CURVE ( 'NONE', #88267, #125403, #104715, .T. ) ;
#62882=EDGE_CURVE ( 'NONE', #81729, #122429, #115552, .T. ) ;
#62885=ORIENTED_EDGE ( 'NONE', *, *, #141195, .F. ) ;
#62888=CARTESIAN_POINT ( 'NONE',  ( 4.110173228882081808, -22.22499999999999787, 4.785647885939356527 ) ) ;
#62889=CARTESIAN_POINT ( 'NONE',  ( 38.99451991528749062, 28.92564299267965211, 4.000000000000000000 ) ) ;
#62890=VECTOR ( 'NONE', #59923, 1000.000000000000000 ) ;
#62892=VECTOR ( 'NONE', #118740, 1000.000000000000227 ) ;
#62893=VECTOR ( 'NONE', #14859, 1000.000000000000000 ) ;
#62894=CARTESIAN_POINT ( 'NONE',  ( 42.18398860626899705, 28.73617430169816700, 5.000000000000000000 ) ) ;
#62895=ORIENTED_EDGE ( 'NONE', *, *, #17488, .T. ) ;
#62897=LINE ( 'NONE', #54178, #31015 ) ;
#62898=FACE_OUTER_BOUND ( 'NONE', #109496, .T. ) ;
#62899=EDGE_LOOP ( 'NONE', ( #38137, #80262, #119342, #42559 ) ) ;
#62900=CARTESIAN_POINT ( 'NONE',  ( -13.44665057663210028, 2.259292476615697876, 14.86850063742357619 ) ) ;
#62901=ORIENTED_EDGE ( 'NONE', *, *, #58459, .T. ) ;
#62902=CARTESIAN_POINT ( 'NONE',  ( -39.18398860626899705, 28.73617430169814568, 5.000000000000000000 ) ) ;
#62903=ORIENTED_EDGE ( 'NONE', *, *, #87073, .T. ) ;
#62904=VECTOR ( 'NONE', #30742, 1000.000000000000000 ) ;
#62906=EDGE_CURVE ( 'NONE', #92329, #91589, #40899, .T. ) ;
#62908=VERTEX_POINT ( 'NONE', #85104 ) ;
#62909=EDGE_CURVE ( 'NONE', #27017, #141849, #93839, .T. ) ;
#62911=EDGE_CURVE ( 'NONE', #49447, #57736, #29292, .T. ) ;
#62912=PLANE ( 'NONE',  #12598 ) ;
#62914=DIRECTION ( 'NONE',  ( -0.7071067811865486830, -0.7071067811865464625, 0.000000000000000000 ) ) ;
#62915=VECTOR ( 'NONE', #86597, 1000.000000000000000 ) ;
#62916=DIRECTION ( 'NONE',  ( -0.6830127018922181881, 0.6830127018922202975, -0.2588190451025214056 ) ) ;
#62917=LINE ( 'NONE', #107093, #122790 ) ;
#62918=ADVANCED_FACE ( 'NONE', ( #52467 ), #107565, .F. ) ;
#62919=DIRECTION ( 'NONE',  ( 0.6830127018922181881, 0.6830127018922202975, -0.2588190451025214056 ) ) ;
#62920=CARTESIAN_POINT ( 'NONE',  ( -27.48921356237309155, -27.52281430457074762, 5.000000000000000000 ) ) ;
#62921=VECTOR ( 'NONE', #105105, 1000.000000000000227 ) ;
#62922=PLANE ( 'NONE',  #86818 ) ;
#62923=ORIENTED_EDGE ( 'NONE', *, *, #39874, .F. ) ;
#62924=DIRECTION ( 'NONE',  ( -0.000000000000000000, 0.000000000000000000, 1.000000000000000000 ) ) ;
#62926=EDGE_LOOP ( 'NONE', ( #79964, #47499, #139014, #138276 ) ) ;
#62927=VECTOR ( 'NONE', #10613, 1000.000000000000000 ) ;
#62928=VERTEX_POINT ( 'NONE', #28607 ) ;
#62930=EDGE_LOOP ( 'NONE', ( #1178, #5360, #79623, #66525 ) ) ;
#62931=CARTESIAN_POINT ( 'NONE',  ( 8.671830600776411657, -15.74070752338412049, 4.000000000000000000 ) ) ;
#62932=DIRECTION ( 'NONE',  ( -0.7071067811865486830, -0.7071067811865464625, -0.000000000000000000 ) ) ;
#62933=CARTESIAN_POINT ( 'NONE',  ( -33.29974487139158867, -27.71228299555229313, 4.000000000000000000 ) ) ;
#62934=VERTEX_POINT ( 'NONE', #5381 ) ;
#62936=VERTEX_POINT ( 'NONE', #106113 ) ;
#62938=( BOUNDED_CURVE ( )  B_SPLINE_CURVE ( 3, ( #50125, #7290, #39986, #84203 ),
 .UNSPECIFIED., .F., .T. ) 
 B_SPLINE_CURVE_WITH_KNOTS ( ( 4, 4 ),
 ( 5.135034128376270601, 5.164990091338616196 ),
 .UNSPECIFIED. ) 
 CURVE ( )  GEOMETRIC_REPRESENTATION_ITEM ( )  RATIONAL_B_SPLINE_CURVE ( ( 1.000000000000000000, 0.9999252214215840207, 0.9999252214215840207, 1.000000000000000000 ) ) 
 REPRESENTATION_ITEM ( '' )  );
#62940=DIRECTION ( 'NONE',  ( -0.7071067811865486830, -0.7071067811865464625, 0.000000000000000000 ) ) ;
#62941=DIRECTION ( 'NONE',  ( -0.7071067811865486830, -0.7071067811865464625, 0.000000000000000000 ) ) ;
#62943=ORIENTED_EDGE ( 'NONE', *, *, #2512, .T. ) ;
#62944=ORIENTED_EDGE ( 'NONE', *, *, #130924, .T. ) ;
#62945=EDGE_CURVE ( 'NONE', #114730, #90903, #102295, .T. ) ;
#62946=VECTOR ( 'NONE', #140545, 1000.000000000000000 ) ;
#62947=ORIENTED_EDGE ( 'NONE', *, *, #76028, .T. ) ;
#62948=PLANE ( 'NONE',  #118134 ) ;
#62949=CARTESIAN_POINT ( 'NONE',  ( 23.99999999999983658, -7.447814304570756327, 5.000000000000000000 ) ) ;
#62950=CARTESIAN_POINT ( 'NONE',  ( -45.48921356237309510, -27.52281430457087197, 5.000000000000000000 ) ) ;
#62952=CARTESIAN_POINT ( 'NONE',  ( -14.48334561358944761, 22.22500000000000142, 4.500000000000000888 ) ) ;
#62953=DIRECTION ( 'NONE',  ( -0.6830127018922181881, 0.6830127018922202975, -0.2588190451025214056 ) ) ;
#62954=CARTESIAN_POINT ( 'NONE',  ( 34.92499999999998295, -13.29806943317888468, 4.500000000000000888 ) ) ;
#62955=CARTESIAN_POINT ( 'NONE',  ( -8.292893218813391698, -3.740707523384241728, 5.000000000000000000 ) ) ;
#62956=LINE ( 'NONE', #41165, #22928 ) ;
#62958=DIRECTION ( 'NONE',  ( -0.000000000000000000, -0.3543493200069152693, 0.9351131265310292928 ) ) ;
#62959=CARTESIAN_POINT ( 'NONE',  ( 15.47336096364205638, -5.240707523384225297, 16.25846745537499416 ) ) ;
#62960=EDGE_LOOP ( 'NONE', ( #60309, #15246, #93423, #89099 ) ) ;
#62961=DIRECTION ( 'NONE',  ( -0.7071067811865486830, -0.7071067811865464625, -0.000000000000000000 ) ) ;
#62963=CARTESIAN_POINT ( 'NONE',  ( -2.999999999999985345, 4.965500833774324718, -4.007596771432649696 ) ) ;
#62964=ORIENTED_EDGE ( 'NONE', *, *, #109458, .T. ) ;
#62965=EDGE_CURVE ( 'NONE', #121666, #91502, #73534, .T. ) ;
#62966=CARTESIAN_POINT ( 'NONE',  ( 33.70701326429281153, -21.74070752338406365, 4.999753212805220670 ) ) ;
#62968=EDGE_LOOP ( 'NONE', ( #111817, #34611, #86030, #114375 ) ) ;
#62969=EDGE_CURVE ( 'NONE', #62317, #20476, #83720, .T. ) ;
#62970=CYLINDRICAL_SURFACE ( 'NONE', #97825, 0.5000000000000004441 ) ;
#62971=DIRECTION ( 'NONE',  ( -0.7071067811865487940, 0.7071067811865463515, 0.000000000000000000 ) ) ;
#62972=AXIS2_PLACEMENT_3D ( 'NONE', #52936, #21032, #87025 ) ;
#62973=ORIENTED_EDGE ( 'NONE', *, *, #50684, .T. ) ;
#62975=ORIENTED_EDGE ( 'NONE', *, *, #97632, .T. ) ;
#62976=EDGE_CURVE ( 'NONE', #36166, #85105, #38753, .T. ) ;
#62977=EDGE_CURVE ( 'NONE', #119390, #63799, #94537, .T. ) ;
#62980=CARTESIAN_POINT ( 'NONE',  ( 2.816011393730999401, 28.73617430169785436, 5.000000000000000000 ) ) ;
#62981=CARTESIAN_POINT ( 'NONE',  ( 41.99451991528749062, 28.92564299267967343, 4.000000000000000000 ) ) ;
#62982=EDGE_CURVE ( 'NONE', #81345, #138649, #7526, .T. ) ;
#62983=CARTESIAN_POINT ( 'NONE',  ( 23.99451991528749062, 28.92564299267954908, 4.000000000000000000 ) ) ;
#62984=FACE_OUTER_BOUND ( 'NONE', #78108, .T. ) ;
#62988=VECTOR ( 'NONE', #46021, 999.9999999999998863 ) ;
#62989=DIRECTION ( 'NONE',  ( -0.6830127018922181881, 0.6830127018922202975, -0.2588190451025214056 ) ) ;
#62990=DIRECTION ( 'NONE',  ( 0.7071067811865486830, -0.7071067811865464625, -0.000000000000000000 ) ) ;
#62991=ORIENTED_EDGE ( 'NONE', *, *, #85735, .T. ) ;
#62994=ADVANCED_FACE ( 'NONE', ( #8224 ), #82979, .F. ) ;
#62996=FACE_OUTER_BOUND ( 'NONE', #117086, .T. ) ;
#62998=DIRECTION ( 'NONE',  ( -1.000000000000000000, 0.000000000000000000, 0.000000000000000000 ) ) ;
#62999=EDGE_CURVE ( 'NONE', #63322, #97308, #17683, .T. ) ;
#63000=CARTESIAN_POINT ( 'NONE',  ( -10.82816939922345867, -20.24070752338406720, 4.000000000000000000 ) ) ;
#63001=DIRECTION ( 'NONE',  ( -0.6830127018922181881, 0.6830127018922202975, -0.2588190451025214056 ) ) ;
#63002=VECTOR ( 'NONE', #34450, 1000.000000000000227 ) ;
#63003=VECTOR ( 'NONE', #63412, 1000.000000000000000 ) ;
#63004=CARTESIAN_POINT ( 'NONE',  ( -13.49999999999990052, 10.46639925780215918, 5.000000000000000000 ) ) ;
#63005=EDGE_LOOP ( 'NONE', ( #74253, #113188, #23778, #3552 ) ) ;
#63006=EDGE_CURVE ( 'NONE', #58831, #37040, #62657, .T. ) ;
#63007=PLANE ( 'NONE',  #48769 ) ;
#63008=DIRECTION ( 'NONE',  ( 0.7071067811865486830, -0.7071067811865464625, -0.000000000000000000 ) ) ;
#63011=CARTESIAN_POINT ( 'NONE',  ( -19.05000000000000071, 3.174999999999997158, 5.000000000000000000 ) ) ;
#63012=VERTEX_POINT ( 'NONE', #40215 ) ;
#63013=EDGE_CURVE ( 'NONE', #139562, #115190, #140211, .T. ) ;
#63014=CARTESIAN_POINT ( 'NONE',  ( -32.84387692260735747, -22.22499999999999787, 4.000000000000000000 ) ) ;
#63015=LINE ( 'NONE', #115900, #84090 ) ;
#63016=LINE ( 'NONE', #139134, #27091 ) ;
#63017=DIRECTION ( 'NONE',  ( 0.7071067811865487940, 0.7071067811865463515, 0.000000000000000000 ) ) ;
#63020=VERTEX_POINT ( 'NONE', #95973 ) ;
#63022=VERTEX_POINT ( 'NONE', #19137 ) ;
#63023=EDGE_CURVE ( 'NONE', #38372, #68590, #62377, .T. ) ;
#63024=LINE ( 'NONE', #44866, #34090 ) ;
#63025=CARTESIAN_POINT ( 'NONE',  ( 27.83652871126532347, 15.75929247661555976, 9.299976744542982843 ) ) ;
#63026=VERTEX_POINT ( 'NONE', #76393 ) ;
#63027=CARTESIAN_POINT ( 'NONE',  ( -33.32816939922329880, -9.740707523384182664, 4.000000000000000000 ) ) ;
#63028=CARTESIAN_POINT ( 'NONE',  ( 57.48921356237308800, -27.52281430457095368, 5.000000000000000000 ) ) ;
#63029=VECTOR ( 'NONE', #12916, 1000.000000000000227 ) ;
#63030=EDGE_CURVE ( 'NONE', #89838, #29922, #32159, .T. ) ;
#63031=AXIS2_PLACEMENT_3D ( 'NONE', #8761, #97216, #109554 ) ;
#63033=ORIENTED_EDGE ( 'NONE', *, *, #69893, .T. ) ;
#63035=AXIS2_PLACEMENT_3D ( 'NONE', #15250, #71836, #59532 ) ;
#63036=CARTESIAN_POINT ( 'NONE',  ( 78.29974487139158157, -27.71228299555260577, 4.000000000000000000 ) ) ;
#63037=VERTEX_POINT ( 'NONE', #56093 ) ;
#63039=DIRECTION ( 'NONE',  ( -0.7071067811865486830, 0.7071067811865464625, 0.000000000000000000 ) ) ;
#63040=VECTOR ( 'NONE', #14987, 1000.000000000000000 ) ;
#63041=LINE ( 'NONE', #7156, #20744 ) ;
#63042=ADVANCED_FACE ( 'NONE', ( #21287 ), #132210, .T. ) ;
#63044=ORIENTED_EDGE ( 'NONE', *, *, #113862, .F. ) ;
#63045=ORIENTED_EDGE ( 'NONE', *, *, #36689, .F. ) ;
#63046=LINE ( 'NONE', #13598, #54107 ) ;
#63047=CARTESIAN_POINT ( 'NONE',  ( 34.92499999999998295, 19.51246187583928204, 4.000000000000000000 ) ) ;
#63049=VECTOR ( 'NONE', #40089, 1000.000000000000000 ) ;
#63050=FACE_OUTER_BOUND ( 'NONE', #107931, .T. ) ;
#63052=ORIENTED_EDGE ( 'NONE', *, *, #58710, .T. ) ;
#63053=EDGE_LOOP ( 'NONE', ( #114580, #84250, #71664, #60262 ) ) ;
#63054=EDGE_CURVE ( 'NONE', #99130, #21326, #77126, .T. ) ;
#63055=DIRECTION ( 'NONE',  ( -0.7071067811865486830, -0.7071067811865464625, -0.000000000000000000 ) ) ;
#63056=ORIENTED_EDGE ( 'NONE', *, *, #71990, .F. ) ;
#63057=ORIENTED_EDGE ( 'NONE', *, *, #71358, .T. ) ;
#63058=VECTOR ( 'NONE', #24321, 1000.000000000000227 ) ;
#63060=EDGE_CURVE ( 'NONE', #122495, #93029, #3183, .T. ) ;
#63063=DIRECTION ( 'NONE',  ( -0.3543493200069163795, -9.265275131829747941E-33, -0.9351131265310288487 ) ) ;
#63064=CARTESIAN_POINT ( 'NONE',  ( 4.828169399223495084, 3.759292476615671230, 4.000000000000000000 ) ) ;
#63065=DIRECTION ( 'NONE',  ( -0.3543493200069162685, -0.000000000000000000, -0.9351131265310288487 ) ) ;
#63069=ORIENTED_EDGE ( 'NONE', *, *, #108275, .F. ) ;
#63070=CARTESIAN_POINT ( 'NONE',  ( -15.18398860626900237, 28.73617430169797871, 5.000000000000000000 ) ) ;
#63071=FACE_BOUND ( 'NONE', #84559, .T. ) ;
#63072=ORIENTED_EDGE ( 'NONE', *, *, #42409, .T. ) ;
#63073=DIRECTION ( 'NONE',  ( 0.7071067811865487940, 0.7071067811865463515, 0.000000000000000000 ) ) ;
#63074=CARTESIAN_POINT ( 'NONE',  ( 36.18398860626899705, 28.73617430169812437, 5.000000000000000000 ) ) ;
#63075=DIRECTION ( 'NONE',  ( -0.7071067811865486830, -0.7071067811865464625, -0.000000000000000000 ) ) ;
#63076=ORIENTED_EDGE ( 'NONE', *, *, #114054, .F. ) ;
#63078=ORIENTED_EDGE ( 'NONE', *, *, #37604, .T. ) ;
#63081=VERTEX_POINT ( 'NONE', #9675 ) ;
#63082=ADVANCED_FACE ( 'NONE', ( #110405 ), #141648, .T. ) ;
#63083=FACE_OUTER_BOUND ( 'NONE', #100163, .T. ) ;
#63084=CARTESIAN_POINT ( 'NONE',  ( 22.49999999999984368, 14.14708470758593251, -0.5283514160167069873 ) ) ;
#63085=CARTESIAN_POINT ( 'NONE',  ( -21.18398860626899349, 28.73617430169802134, 5.000000000000000000 ) ) ;
#63086=LINE ( 'NONE', #107259, #84401 ) ;
#63087=DIRECTION ( 'NONE',  ( -0.7071067811865486830, -0.7071067811865464625, -0.000000000000000000 ) ) ;
#63088=LINE ( 'NONE', #107262, #73690 ) ;
#63090=VECTOR ( 'NONE', #23506, 1000.000000000000227 ) ;
#63092=CARTESIAN_POINT ( 'NONE',  ( -34.49999999999975842, 14.14708470758588099, -0.5283514160165768692 ) ) ;
#63093=VECTOR ( 'NONE', #75755, 1000.000000000000000 ) ;
#63094=VECTOR ( 'NONE', #26837, 1000.000000000000000 ) ;
#63095=FACE_OUTER_BOUND ( 'NONE', #100966, .T. ) ;
#63096=CARTESIAN_POINT ( 'NONE',  ( -1.734723475976807094E-15, 19.93112307739198386, 4.000000000000000000 ) ) ;
#63097=DIRECTION ( 'NONE',  ( 0.7071067811865486830, -0.7071067811865464625, -0.000000000000000000 ) ) ;
#63098=VERTEX_POINT ( 'NONE', #75674 ) ;
#63100=AXIS2_PLACEMENT_3D ( 'NONE', #124143, #1612, #100953 ) ;
#63101=ORIENTED_EDGE ( 'NONE', *, *, #46556, .F. ) ;
#63103=ORIENTED_EDGE ( 'NONE', *, *, #56423, .F. ) ;
#63106=EDGE_LOOP ( 'NONE', ( #49300, #64700, #74529, #115635 ) ) ;
#63107=EDGE_LOOP ( 'NONE', ( #127532, #111341, #56392, #118889 ) ) ;
#63108=PLANE ( 'NONE',  #472 ) ;
#63110=DIRECTION ( 'NONE',  ( 0.000000000000000000, -0.000000000000000000, -1.000000000000000000 ) ) ;
#63111=ORIENTED_EDGE ( 'NONE', *, *, #81166, .F. ) ;
#63112=CARTESIAN_POINT ( 'NONE',  ( 14.99999999999988809, -10.77435723561694125, -9.972017380717266732 ) ) ;
#63117=ORIENTED_EDGE ( 'NONE', *, *, #78037, .T. ) ;
#63120=LINE ( 'NONE', #61688, #88348 ) ;
#63121=LINE ( 'NONE', #97863, #67440 ) ;
#63122=VERTEX_POINT ( 'NONE', #130788 ) ;
#63123=ORIENTED_EDGE ( 'NONE', *, *, #127022, .F. ) ;
#63125=VERTEX_POINT ( 'NONE', #130053 ) ;
#63126=LINE ( 'NONE', #68144, #111063 ) ;
#63127=CARTESIAN_POINT ( 'NONE',  ( 21.08314806772918004, 21.75929247661549581, 7.311836541448100135 ) ) ;
#63128=CARTESIAN_POINT ( 'NONE',  ( -18.47512612785034491, 14.25929247661557575, 9.797011795316594274 ) ) ;
#63129=DIRECTION ( 'NONE',  ( -0.3543493200069162685, -0.000000000000000000, -0.9351131265310288487 ) ) ;
#63130=VERTEX_POINT ( 'NONE', #44501 ) ;
#63132=FACE_OUTER_BOUND ( 'NONE', #69333, .T. ) ;
#63133=VECTOR ( 'NONE', #28137, 1000.000000000000227 ) ;
#63135=DIRECTION ( 'NONE',  ( 0.6830127018922181881, 0.6830127018922202975, -0.2588190451025214056 ) ) ;
#63136=EDGE_CURVE ( 'NONE', #38538, #66120, #42347, .T. ) ;
#63137=ORIENTED_EDGE ( 'NONE', *, *, #604, .T. ) ;
#63138=DIRECTION ( 'NONE',  ( -0.7071067811865486830, -0.7071067811865464625, 0.000000000000000000 ) ) ;
#63139=AXIS2_PLACEMENT_3D ( 'NONE', #93829, #49651, #106833 ) ;
#63140=VECTOR ( 'NONE', #100080, 999.9999999999998863 ) ;
#63141=CARTESIAN_POINT ( 'NONE',  ( 31.17183060077626067, 21.75929247661550647, 4.000000000000000000 ) ) ;
#63142=ORIENTED_EDGE ( 'NONE', *, *, #10112, .T. ) ;
#63143=CARTESIAN_POINT ( 'NONE',  ( -30.18398860626900060, 28.73617430169808173, 5.000000000000000000 ) ) ;
#63145=ORIENTED_EDGE ( 'NONE', *, *, #40458, .F. ) ;
#63146=EDGE_CURVE ( 'NONE', #142010, #76898, #20542, .T. ) ;
#63147=EDGE_CURVE ( 'NONE', #89949, #70280, #19838, .T. ) ;
#63148=FACE_OUTER_BOUND ( 'NONE', #76064, .T. ) ;
#63149=DIRECTION ( 'NONE',  ( -0.7071067811865486830, -0.7071067811865464625, 0.000000000000000000 ) ) ;
#63151=DIRECTION ( 'NONE',  ( -0.3543493200069162685, -0.000000000000000000, -0.9351131265310288487 ) ) ;
#63152=EDGE_CURVE ( 'NONE', #112531, #113476, #64801, .T. ) ;
#63153=EDGE_CURVE ( 'NONE', #86059, #123098, #61614, .T. ) ;
#63155=EDGE_CURVE ( 'NONE', #14007, #139229, #78526, .T. ) ;
#63156=PLANE ( 'NONE',  #80933 ) ;
#63157=LINE ( 'NONE', #8683, #113715 ) ;
#63159=CARTESIAN_POINT ( 'NONE',  ( -3.299744871391591339, -27.71228299555208352, 4.000000000000000000 ) ) ;
#63160=AXIS2_PLACEMENT_3D ( 'NONE', #1801, #47554, #113450 ) ;
#63161=DIRECTION ( 'NONE',  ( 0.3543493200069162685, -0.000000000000000000, -0.9351131265310288487 ) ) ;
#63162=CARTESIAN_POINT ( 'NONE',  ( -17.81601139373099940, 28.73617430169775133, 5.000000000000000000 ) ) ;
#63163=CARTESIAN_POINT ( 'NONE',  ( 8.287690060339658160, -21.73547319004781642, 4.999917730833664642 ) ) ;
#63164=PLANE ( 'NONE',  #134693 ) ;
#63166=DIRECTION ( 'NONE',  ( -0.7071067811865487940, 0.7071067811865463515, -0.000000000000000000 ) ) ;
#63167=ADVANCED_FACE ( 'NONE', ( #91547 ), #13235, .F. ) ;
#63168=CARTESIAN_POINT ( 'NONE',  ( -6.792893218813404133, -2.240707523384255939, 5.000000000000000000 ) ) ;
#63169=CARTESIAN_POINT ( 'NONE',  ( -12.18398860626900060, 28.73617430169795739, 5.000000000000000000 ) ) ;
#63170=VERTEX_POINT ( 'NONE', #28246 ) ;
#63173=EDGE_LOOP ( 'NONE', ( #115435, #8968, #8755, #16734 ) ) ;
#63175=EDGE_CURVE ( 'NONE', #30612, #84615, #133625, .T. ) ;
#63176=VERTEX_POINT ( 'NONE', #57505 ) ;
#63177=ORIENTED_EDGE ( 'NONE', *, *, #95956, .T. ) ;
#63178=ORIENTED_EDGE ( 'NONE', *, *, #94224, .F. ) ;
#63179=CARTESIAN_POINT ( 'NONE',  ( -16.49999999999988276, -5.947814304570758104, 5.000000000000000000 ) ) ;
#63180=CARTESIAN_POINT ( 'NONE',  ( 11.29289321881338282, -15.74070752338412049, 5.000000000000000000 ) ) ;
#63182=VERTEX_POINT ( 'NONE', #67684 ) ;
#63184=PLANE ( 'NONE',  #83307 ) ;
#63185=EDGE_CURVE ( 'NONE', #49545, #63026, #135080, .T. ) ;
#63186=DIRECTION ( 'NONE',  ( 0.6830127018922180770, -0.6830127018922204085, -0.2588190451025213501 ) ) ;
#63187=DIRECTION ( 'NONE',  ( 0.6830127018922180770, -0.6830127018922204085, -0.2588190451025213501 ) ) ;
#63188=PLANE ( 'NONE',  #9515 ) ;
#63190=ORIENTED_EDGE ( 'NONE', *, *, #31901, .T. ) ;
#63192=CARTESIAN_POINT ( 'NONE',  ( -16.49999999999988276, -9.462702396501025959, -9.474982329943475889 ) ) ;
#63193=CARTESIAN_POINT ( 'NONE',  ( -23.95341186370441378, 14.25929247661557042, 18.84478104361333450 ) ) ;
#63195=EDGE_CURVE ( 'NONE', #93386, #51714, #35772, .T. ) ;
#63197=DIRECTION ( 'NONE',  ( -0.6830127018922181881, 0.6830127018922202975, -0.2588190451025214056 ) ) ;
#63198=CARTESIAN_POINT ( 'NONE',  ( 20.99451991528748707, 28.92564299267952777, 4.000000000000000000 ) ) ;
#63200=CARTESIAN_POINT ( 'NONE',  ( 42.18398860626899705, 28.73617430169816700, 5.000000000000000000 ) ) ;
#63202=ORIENTED_EDGE ( 'NONE', *, *, #72131, .F. ) ;
#63204=ORIENTED_EDGE ( 'NONE', *, *, #9594, .T. ) ;
#63206=DIRECTION ( 'NONE',  ( -0.7071067811865486830, 0.7071067811865464625, 0.000000000000000000 ) ) ;
#63207=VECTOR ( 'NONE', #37065, 1000.000000000000227 ) ;
#63209=LINE ( 'NONE', #8730, #39921 ) ;
#63210=AXIS2_PLACEMENT_3D ( 'NONE', #86465, #83623, #74890 ) ;
#63211=LINE ( 'NONE', #41409, #104521 ) ;
#63212=CARTESIAN_POINT ( 'NONE',  ( -20.99999999999984368, -6.412538124160692909, 4.000000000000000000 ) ) ;
#63214=ADVANCED_FACE ( 'NONE', ( #79990 ), #124879, .F. ) ;
#63216=ORIENTED_EDGE ( 'NONE', *, *, #77063, .F. ) ;
#63217=EDGE_CURVE ( 'NONE', #65963, #142366, #39121, .T. ) ;
#63218=DIRECTION ( 'NONE',  ( 0.6830127018922180770, -0.6830127018922204085, -0.2588190451025213501 ) ) ;
#63219=EDGE_LOOP ( 'NONE', ( #111378, #14610, #65148, #8027 ) ) ;
#63220=AXIS2_PLACEMENT_3D ( 'NONE', #93400, #139791, #7791 ) ;
#63221=VECTOR ( 'NONE', #129473, 1000.000000000000227 ) ;
#63223=LINE ( 'NONE', #64608, #52435 ) ;
#63224=CARTESIAN_POINT ( 'NONE',  ( -33.51665438641022376, 22.22500000000000142, 4.500000000000000888 ) ) ;
#63225=EDGE_CURVE ( 'NONE', #88378, #19029, #60917, .T. ) ;
#63226=EDGE_CURVE ( 'NONE', #106843, #83227, #72507, .T. ) ;
#63227=DIRECTION ( 'NONE',  ( 0.6830127018922180770, -0.6830127018922204085, -0.2588190451025213501 ) ) ;
#63228=EDGE_LOOP ( 'NONE', ( #39962, #53089, #66025, #69473, #12479 ) ) ;
#63230=ORIENTED_EDGE ( 'NONE', *, *, #92485, .T. ) ;
#63231=CARTESIAN_POINT ( 'NONE',  ( -45.29974487139158867, -27.71228299555237840, 4.000000000000000000 ) ) ;
#63232=LINE ( 'NONE', #63914, #20776 ) ;
#63233=CARTESIAN_POINT ( 'NONE',  ( 1.499999999999990896, -2.947814304570802513, 5.000000000000000000 ) ) ;
#63235=VECTOR ( 'NONE', #73637, 1000.000000000000000 ) ;
#63238=EDGE_CURVE ( 'NONE', #33598, #103136, #105078, .T. ) ;
#63239=CARTESIAN_POINT ( 'NONE',  ( -7.499999999999949374, 16.77039438581778796, 0.4657186855307913764 ) ) ;
#63240=VERTEX_POINT ( 'NONE', #116668 ) ;
#63241=ORIENTED_EDGE ( 'NONE', *, *, #52322, .T. ) ;
#63242=EDGE_LOOP ( 'NONE', ( #23251, #52727, #86871, #45378 ) ) ;
#63243=AXIS2_PLACEMENT_3D ( 'NONE', #46345, #47086, #15082 ) ;
#63244=CARTESIAN_POINT ( 'NONE',  ( 0.000000000000000000, 0.000000000000000000, 5.000000000000000000 ) ) ;
#63248=EDGE_CURVE ( 'NONE', #87783, #100682, #102440, .T. ) ;
#63249=VERTEX_POINT ( 'NONE', #68394 ) ;
#63250=VECTOR ( 'NONE', #65638, 1000.000000000000000 ) ;
#63251=CARTESIAN_POINT ( 'NONE',  ( 17.92867102513379862, 9.037728232668255757, 5.000000000000000000 ) ) ;
#63252=DIRECTION ( 'NONE',  ( -0.000000000000000000, 0.000000000000000000, 1.000000000000000000 ) ) ;
#63253=CARTESIAN_POINT ( 'NONE',  ( 13.20450575203696886, 4.382956123802139281, 4.000000000000000000 ) ) ;
#63255=FACE_BOUND ( 'NONE', #19311, .T. ) ;
#63256=ORIENTED_EDGE ( 'NONE', *, *, #15469, .F. ) ;
#63259=VERTEX_POINT ( 'NONE', #5740 ) ;
#63260=DIRECTION ( 'NONE',  ( 0.7071067811865487940, 0.7071067811865463515, 0.000000000000000000 ) ) ;
#63261=ORIENTED_EDGE ( 'NONE', *, *, #38299, .T. ) ;
#63262=ORIENTED_EDGE ( 'NONE', *, *, #59661, .T. ) ;
#63263=FACE_OUTER_BOUND ( 'NONE', #40270, .T. ) ;
#63264=VERTEX_POINT ( 'NONE', #94190 ) ;
#63265=AXIS2_PLACEMENT_3D ( 'NONE', #91316, #74378, #91992 ) ;
#63267=ORIENTED_EDGE ( 'NONE', *, *, #86450, .T. ) ;
#63268=CARTESIAN_POINT ( 'NONE',  ( 21.29974487139158512, -27.71228299555221142, 4.000000000000000000 ) ) ;
#63269=LINE ( 'NONE', #40776, #75096 ) ;
#63271=ORIENTED_EDGE ( 'NONE', *, *, #135363, .F. ) ;
#63272=CARTESIAN_POINT ( 'NONE',  ( 60.18398860626900415, 28.73617430169829490, 5.000000000000000000 ) ) ;
#63273=AXIS2_PLACEMENT_3D ( 'NONE', #52441, #96629, #40190 ) ;
#63274=EDGE_CURVE ( 'NONE', #1311, #94958, #62491, .T. ) ;
#63275=EDGE_CURVE ( 'NONE', #141681, #1315, #23409, .T. ) ;
#63276=CARTESIAN_POINT ( 'NONE',  ( 33.48921356237309510, -27.52281430457078670, 5.000000000000000000 ) ) ;
#63278=CARTESIAN_POINT ( 'NONE',  ( -5.292893218813412126, 11.25929247661560240, 5.000000000000000000 ) ) ;
#63279=DIRECTION ( 'NONE',  ( -0.7071067811865487940, 0.7071067811865463515, 0.000000000000000000 ) ) ;
#63280=FACE_OUTER_BOUND ( 'NONE', #143346, .T. ) ;
#63281=EDGE_LOOP ( 'NONE', ( #15902, #6204, #11036, #54792 ) ) ;
#63282=VECTOR ( 'NONE', #91780, 1000.000000000000000 ) ;
#63285=LINE ( 'NONE', #8115, #130025 ) ;
#63286=ORIENTED_EDGE ( 'NONE', *, *, #58465, .T. ) ;
#63287=ORIENTED_EDGE ( 'NONE', *, *, #93603, .T. ) ;
#63288=ORIENTED_EDGE ( 'NONE', *, *, #138786, .F. ) ;
#63289=CARTESIAN_POINT ( 'NONE',  ( 33.48921356237309510, -27.52281430457078670, 5.000000000000000000 ) ) ;
#63291=ADVANCED_FACE ( 'NONE', ( #28955 ), #107900, .F. ) ;
#63292=DIRECTION ( 'NONE',  ( -0.7071067811865486830, -0.7071067811865464625, 0.000000000000000000 ) ) ;
#63295=CARTESIAN_POINT ( 'NONE',  ( 39.29974487139159578, -27.71228299555233576, 4.000000000000000000 ) ) ;
#63296=CARTESIAN_POINT ( 'NONE',  ( -34.92500000000001137, -22.22500000000000142, 4.000000000000000000 ) ) ;
#63298=CARTESIAN_POINT ( 'NONE',  ( -5.816011393731002066, 28.73617430169783304, 5.000000000000000000 ) ) ;
#63299=VERTEX_POINT ( 'NONE', #118805 ) ;
#63301=DIRECTION ( 'NONE',  ( 0.7071067811865487940, 0.7071067811865463515, 0.000000000000000000 ) ) ;
#63302=CARTESIAN_POINT ( 'NONE',  ( 14.29289321881336150, -0.7407075233842770334, 5.000000000000000000 ) ) ;
#63303=AXIS2_PLACEMENT_3D ( 'NONE', #1384, #45671, #13688 ) ;
#63304=LINE ( 'NONE', #119059, #40254 ) ;
#63306=CARTESIAN_POINT ( 'NONE',  ( -11.99451991528749417, 28.92564299267946382, 4.000000000000000000 ) ) ;
#63307=ORIENTED_EDGE ( 'NONE', *, *, #70036, .F. ) ;
#63308=FACE_OUTER_BOUND ( 'NONE', #84481, .T. ) ;
#63309=CARTESIAN_POINT ( 'NONE',  ( -10.49999999999992539, -14.56887692260766087, 4.000000000000000000 ) ) ;
#63310=DIRECTION ( 'NONE',  ( -0.7071067811865487940, 0.7071067811865463515, 0.000000000000000000 ) ) ;
#63311=AXIS2_PLACEMENT_3D ( 'NONE', #77696, #68278, #58112 ) ;
#63312=ORIENTED_EDGE ( 'NONE', *, *, #112598, .T. ) ;
#63313=DIRECTION ( 'NONE',  ( 0.6830127018922181881, 0.6830127018922202975, -0.2588190451025214056 ) ) ;
#63314=CARTESIAN_POINT ( 'NONE',  ( 44.99451991528749772, 28.92564299267969474, 4.000000000000000000 ) ) ;
#63315=CARTESIAN_POINT ( 'NONE',  ( -34.45011844616454511, 21.00230414159373638, 5.000000000000000888 ) ) ;
#63316=VECTOR ( 'NONE', #131297, 999.9999999999998863 ) ;
#63317=VERTEX_POINT ( 'NONE', #63743 ) ;
#63318=DIRECTION ( 'NONE',  ( -0.000000000000000000, 0.3543493200069153248, 0.9351131265310292928 ) ) ;
#63319=DIRECTION ( 'NONE',  ( -0.6830127018922180770, -0.6830127018922204085, -0.2588190451025213501 ) ) ;
#63321=CARTESIAN_POINT ( 'NONE',  ( 47.99451991528749062, 28.92564299267971251, 4.000000000000000000 ) ) ;
#63322=VERTEX_POINT ( 'NONE', #6423 ) ;
#63323=EDGE_CURVE ( 'NONE', #84062, #95284, #60097, .T. ) ;
#63325=DIRECTION ( 'NONE',  ( 0.3543493200069162685, -0.000000000000000000, -0.9351131265310288487 ) ) ;
#63326=CARTESIAN_POINT ( 'NONE',  ( 11.15971793293161340, -22.22500000000000142, 22.46322236200905209 ) ) ;
#63328=DIRECTION ( 'NONE',  ( 0.7071067811865487940, 0.7071067811865463515, 0.000000000000000000 ) ) ;
#63329=ADVANCED_FACE ( 'NONE', ( #117357 ), #18768, .F. ) ;
#63330=VECTOR ( 'NONE', #140669, 1000.000000000000227 ) ;
#63331=PLANE ( 'NONE',  #64544 ) ;
#63332=LINE ( 'NONE', #139466, #93074 ) ;
#63333=EDGE_CURVE ( 'NONE', #14760, #70281, #63041, .T. ) ;
#63334=ORIENTED_EDGE ( 'NONE', *, *, #40412, .T. ) ;
#63335=EDGE_CURVE ( 'NONE', #5782, #104397, #84760, .T. ) ;
#63336=PLANE ( 'NONE',  #51347 ) ;
#63337=LINE ( 'NONE', #108908, #35493 ) ;
#63338=EDGE_CURVE ( 'NONE', #41423, #54775, #52814, .T. ) ;
#63340=AXIS2_PLACEMENT_3D ( 'NONE', #121370, #131550, #63472 ) ;
#63342=ORIENTED_EDGE ( 'NONE', *, *, #18485, .F. ) ;
#63343=FACE_OUTER_BOUND ( 'NONE', #122808, .T. ) ;
#63344=VECTOR ( 'NONE', #60188, 1000.000000000000227 ) ;
#63345=ORIENTED_EDGE ( 'NONE', *, *, #54856, .F. ) ;
#63346=EDGE_CURVE ( 'NONE', #36068, #10862, #41984, .T. ) ;
#63347=ORIENTED_EDGE ( 'NONE', *, *, #93914, .F. ) ;
#63348=DIRECTION ( 'NONE',  ( 0.3543493200069162685, -0.000000000000000000, -0.9351131265310288487 ) ) ;
#63350=ORIENTED_EDGE ( 'NONE', *, *, #78572, .T. ) ;
#63351=DIRECTION ( 'NONE',  ( 0.7071067811865487940, -0.7071067811865463515, 0.000000000000000000 ) ) ;
#63352=CARTESIAN_POINT ( 'NONE',  ( -31.49999999999977973, -4.533600742197687161, 5.000000000000000000 ) ) ;
#63354=ADVANCED_FACE ( 'NONE', ( #108608 ), #96307, .F. ) ;
#63355=CARTESIAN_POINT ( 'NONE',  ( 57.18398860626899705, 28.73617430169827358, 5.000000000000000000 ) ) ;
#63356=EDGE_CURVE ( 'NONE', #10452, #93773, #30375, .T. ) ;
#63358=CARTESIAN_POINT ( 'NONE',  ( -3.183988606268992161, 28.73617430169789699, 5.000000000000000000 ) ) ;
#63360=CARTESIAN_POINT ( 'NONE',  ( -3.469446951953614189E-15, 4.965500833774328271, -4.007596771432656801 ) ) ;
#63362=DIRECTION ( 'NONE',  ( -0.000000000000000000, 0.3543493200069153248, 0.9351131265310292928 ) ) ;
#63363=CARTESIAN_POINT ( 'NONE',  ( -5.588385094051650626, 22.22500000000000142, 4.777194822843815913 ) ) ;
#63366=AXIS2_PLACEMENT_3D ( 'NONE', #52683, #30967, #109212 ) ;
#63369=DIRECTION ( 'NONE',  ( 0.7071067811865487940, 0.7071067811865463515, 0.000000000000000000 ) ) ;
#63370=EDGE_LOOP ( 'NONE', ( #122628, #29307, #20630, #53708 ) ) ;
#63374=DIRECTION ( 'NONE',  ( 0.7071067811865487940, 0.7071067811865463515, 0.000000000000000000 ) ) ;
#63377=ORIENTED_EDGE ( 'NONE', *, *, #114002, .F. ) ;
#63380=ORIENTED_EDGE ( 'NONE', *, *, #115404, .T. ) ;
#63381=ADVANCED_FACE ( 'NONE', ( #119494 ), #40557, .T. ) ;
#63383=EDGE_LOOP ( 'NONE', ( #46728, #65220, #13769, #135220 ) ) ;
#63384=ORIENTED_EDGE ( 'NONE', *, *, #74624, .T. ) ;
#63388=CYLINDRICAL_SURFACE ( 'NONE', #48931, 0.5000000000000004441 ) ;
#63391=DIRECTION ( 'NONE',  ( -0.3543493200069163240, 0.000000000000000000, 0.9351131265310288487 ) ) ;
#63393=ORIENTED_EDGE ( 'NONE', *, *, #12875, .F. ) ;
#63395=CARTESIAN_POINT ( 'NONE',  ( -2.816011393730999401, 28.73617430169785436, 5.000000000000000000 ) ) ;
#63397=CARTESIAN_POINT ( 'NONE',  ( -57.18398860626899705, 28.73617430169827358, 5.000000000000000000 ) ) ;
#63398=DIRECTION ( 'NONE',  ( 0.7071067811865487940, 0.7071067811865463515, 0.000000000000000000 ) ) ;
#63399=EDGE_CURVE ( 'NONE', #107560, #132680, #73194, .T. ) ;
#63400=ORIENTED_EDGE ( 'NONE', *, *, #84852, .T. ) ;
#63401=ORIENTED_EDGE ( 'NONE', *, *, #26593, .F. ) ;
#63403=DIRECTION ( 'NONE',  ( 0.7071067811865486830, -0.7071067811865464625, -0.000000000000000000 ) ) ;
#63405=CARTESIAN_POINT ( 'NONE',  ( -27.32816939922334143, -6.740707523384214639, 4.000000000000000000 ) ) ;
#63407=CARTESIAN_POINT ( 'NONE',  ( 8.671830600776416986, -9.740707523384180888, 4.000000000000000000 ) ) ;
#63408=FACE_OUTER_BOUND ( 'NONE', #70356, .T. ) ;
#63409=ORIENTED_EDGE ( 'NONE', *, *, #82838, .T. ) ;
#63410=ORIENTED_EDGE ( 'NONE', *, *, #67932, .F. ) ;
#63411=LINE ( 'NONE', #87978, #44755 ) ;
#63412=DIRECTION ( 'NONE',  ( 0.7071067811865486830, -0.7071067811865464625, -0.000000000000000000 ) ) ;
#63413=ORIENTED_EDGE ( 'NONE', *, *, #95698, .T. ) ;
#63414=VECTOR ( 'NONE', #44905, 1000.000000000000000 ) ;
#63415=VERTEX_POINT ( 'NONE', #95626 ) ;
#63416=EDGE_CURVE ( 'NONE', #89630, #137664, #139880, .T. ) ;
#63417=DIRECTION ( 'NONE',  ( -0.7071067811865487940, 0.7071067811865463515, 0.000000000000000000 ) ) ;
#63419=CARTESIAN_POINT ( 'NONE',  ( 17.66989781452724984, 17.25929247661554555, 19.83885114516067105 ) ) ;
#63421=CARTESIAN_POINT ( 'NONE',  ( -34.92500000000001137, -17.24070752338410628, 4.255531930566259113 ) ) ;
#63422=ADVANCED_FACE ( 'NONE', ( #77026 ), #119061, .T. ) ;
#63423=FACE_BOUND ( 'NONE', #118210, .T. ) ;
#63424=DIRECTION ( 'NONE',  ( 0.3543493200069162685, -0.000000000000000000, -0.9351131265310288487 ) ) ;
#63426=CARTESIAN_POINT ( 'NONE',  ( -15.70710678118643422, 8.259292476615641476, 5.000000000000000000 ) ) ;
#63427=LINE ( 'NONE', #75007, #108268 ) ;
#63428=ORIENTED_EDGE ( 'NONE', *, *, #8250, .F. ) ;
#63429=VECTOR ( 'NONE', #124908, 1000.000000000000000 ) ;
#63430=CARTESIAN_POINT ( 'NONE',  ( -14.99999999999989164, -15.03360074219758857, 5.000000000000000000 ) ) ;
#63432=ORIENTED_EDGE ( 'NONE', *, *, #70184, .F. ) ;
#63434=VERTEX_POINT ( 'NONE', #121199 ) ;
#63436=ORIENTED_EDGE ( 'NONE', *, *, #34819, .F. ) ;
#63437=FACE_OUTER_BOUND ( 'NONE', #112700, .T. ) ;
#63439=AXIS2_PLACEMENT_3D ( 'NONE', #10292, #132107, #98727 ) ;
#63440=PLANE ( 'NONE',  #65649 ) ;
#63441=DIRECTION ( 'NONE',  ( 0.7071067811865487940, 0.7071067811865463515, -0.000000000000000000 ) ) ;
#63444=VECTOR ( 'NONE', #20284, 1000.000000000000227 ) ;
#63445=LINE ( 'NONE', #107612, #78292 ) ;
#63446=CARTESIAN_POINT ( 'NONE',  ( -69.29974487139159578, -27.71228299555254537, 4.000000000000000000 ) ) ;
#63451=CARTESIAN_POINT ( 'NONE',  ( -17.95341186370444930, 14.25929247661557753, 18.84478104361332385 ) ) ;
#63452=CARTESIAN_POINT ( 'NONE',  ( -14.99999999999988987, -9.033600742197641864, 5.000000000000000000 ) ) ;
#63453=VECTOR ( 'NONE', #104637, 1000.000000000000227 ) ;
#63454=ORIENTED_EDGE ( 'NONE', *, *, #41107, .F. ) ;
#63455=VERTEX_POINT ( 'NONE', #8821 ) ;
#63456=AXIS2_PLACEMENT_3D ( 'NONE', #93585, #127645, #37051 ) ;
#63458=EDGE_LOOP ( 'NONE', ( #90001, #66810, #133680, #113218 ) ) ;
#63462=VECTOR ( 'NONE', #50753, 1000.000000000000000 ) ;
#63463=VECTOR ( 'NONE', #136172, 1000.000000000000000 ) ;
#63466=VERTEX_POINT ( 'NONE', #19042 ) ;
#63467=CARTESIAN_POINT ( 'NONE',  ( 0.000000000000000000, 0.000000000000000000, 5.000000000000000000 ) ) ;
#63468=ORIENTED_EDGE ( 'NONE', *, *, #77784, .T. ) ;
#63469=CARTESIAN_POINT ( 'NONE',  ( 34.42499999999998295, 21.72500000000000142, 0.5000000000000000000 ) ) ;
#63470=VECTOR ( 'NONE', #51917, 1000.000000000000227 ) ;
#63471=FACE_OUTER_BOUND ( 'NONE', #125278, .T. ) ;
#63472=DIRECTION ( 'NONE',  ( -0.7071067811865486830, 0.7071067811865464625, 0.000000000000000000 ) ) ;
#63473=ORIENTED_EDGE ( 'NONE', *, *, #14016, .F. ) ;
#63474=VERTEX_POINT ( 'NONE', #41500 ) ;
#63476=CARTESIAN_POINT ( 'NONE',  ( -60.48921356237309510, -27.52281430457097500, 5.000000000000000000 ) ) ;
#63477=LINE ( 'NONE', #107643, #42539 ) ;
#63478=ORIENTED_EDGE ( 'NONE', *, *, #30496, .T. ) ;
#63481=VERTEX_POINT ( 'NONE', #74887 ) ;
#63482=VERTEX_POINT ( 'NONE', #10294 ) ;
#63483=ORIENTED_EDGE ( 'NONE', *, *, #45362, .F. ) ;
#63484=PLANE ( 'NONE',  #118902 ) ;
#63487=CARTESIAN_POINT ( 'NONE',  ( -28.49999999999978684, 19.08746187583905041, 4.000000000000000000 ) ) ;
#63488=CARTESIAN_POINT ( 'NONE',  ( -25.82816939922334853, -20.24070752338407431, 4.000000000000000000 ) ) ;
#63491=CARTESIAN_POINT ( 'NONE',  ( 10.49999999999992895, 12.43112307739206024, 4.000000000000000000 ) ) ;
#63492=ORIENTED_EDGE ( 'NONE', *, *, #11671, .T. ) ;
#63493=LINE ( 'NONE', #96752, #125842 ) ;
#63495=EDGE_CURVE ( 'NONE', #136020, #32222, #109615, .T. ) ;
#63496=VECTOR ( 'NONE', #61853, 1000.000000000000000 ) ;
#63498=CARTESIAN_POINT ( 'NONE',  ( 45.18398860626900415, 28.73617430169818832, 5.000000000000000000 ) ) ;
#63499=CARTESIAN_POINT ( 'NONE',  ( 15.70710678118643955, 17.25929247661554200, 5.000000000000000000 ) ) ;
#63500=ORIENTED_EDGE ( 'NONE', *, *, #57338, .F. ) ;
#63501=ADVANCED_FACE ( 'NONE', ( #52378 ), #132109, .T. ) ;
#63502=ORIENTED_EDGE ( 'NONE', *, *, #116771, .T. ) ;
#63503=CARTESIAN_POINT ( 'NONE',  ( 9.489213562373095101, -27.52281430457062328, 5.000000000000000000 ) ) ;
#63505=ADVANCED_FACE ( 'NONE', ( #64701 ), #87158, .F. ) ;
#63506=LINE ( 'NONE', #74360, #53911 ) ;
#63507=CARTESIAN_POINT ( 'NONE',  ( 16.98012225071442316, -17.24070752338409918, 20.23474786156473115 ) ) ;
#63508=CARTESIAN_POINT ( 'NONE',  ( 22.11017322888194769, -22.22500000000000142, 4.785647885939353863 ) ) ;
#63509=ADVANCED_FACE ( 'NONE', ( #131383 ), #96564, .F. ) ;
#63511=ADVANCED_FACE ( 'NONE', ( #19752 ), #129955, .T. ) ;
#63514=CARTESIAN_POINT ( 'NONE',  ( -18.18398860626898994, 28.73617430169800002, 5.000000000000000000 ) ) ;
#63515=CARTESIAN_POINT ( 'NONE',  ( -33.79289321881321939, 6.759292476615654799, 5.000000000000000000 ) ) ;
#63516=ORIENTED_EDGE ( 'NONE', *, *, #78201, .F. ) ;
#63517=DIRECTION ( 'NONE',  ( -0.7071067811865486830, -0.7071067811865464625, -0.000000000000000000 ) ) ;
#63519=DIRECTION ( 'NONE',  ( -0.000000000000000000, -0.3543493200069152693, 0.9351131265310292928 ) ) ;
#63520=CARTESIAN_POINT ( 'NONE',  ( -34.49999999999975842, 0.4497235411627144019, -5.599840258123620629 ) ) ;
#63521=EDGE_LOOP ( 'NONE', ( #35183, #96771, #98348, #14568 ) ) ;
#63522=DIRECTION ( 'NONE',  ( 0.000000000000000000, 0.000000000000000000, -1.000000000000000000 ) ) ;
#63523=CARTESIAN_POINT ( 'NONE',  ( -45.18398860626900415, 28.73617430169818832, 5.000000000000000000 ) ) ;
#63525=EDGE_CURVE ( 'NONE', #128612, #16746, #53839, .T. ) ;
#63526=CARTESIAN_POINT ( 'NONE',  ( 0.000000000000000000, 0.000000000000000000, 5.000000000000000000 ) ) ;
#63527=EDGE_CURVE ( 'NONE', #7366, #19220, #42961, .T. ) ;
#63528=CARTESIAN_POINT ( 'NONE',  ( -34.92500000000001137, -9.183345613589475320, 4.500000000000000888 ) ) ;
#63529=DIRECTION ( 'NONE',  ( 0.6830127018922180770, -0.6830127018922204085, -0.2588190451025213501 ) ) ;
#63530=EDGE_LOOP ( 'NONE', ( #112128, #8697, #14491, #118101 ) ) ;
#63531=ORIENTED_EDGE ( 'NONE', *, *, #99183, .T. ) ;
#63532=FACE_OUTER_BOUND ( 'NONE', #50021, .T. ) ;
#63535=CARTESIAN_POINT ( 'NONE',  ( 21.70710678118638981, -3.740707523384241728, 5.000000000000000000 ) ) ;
#63536=EDGE_CURVE ( 'NONE', #128596, #60521, #2989, .T. ) ;
#63538=DIRECTION ( 'NONE',  ( -0.000000000000000000, 0.3543493200069153248, 0.9351131265310292928 ) ) ;
#63539=AXIS2_PLACEMENT_3D ( 'NONE', #46233, #123056, #15663 ) ;
#63540=DIRECTION ( 'NONE',  ( 0.3543493200069163240, 0.000000000000000000, 0.9351131265310288487 ) ) ;
#63541=EDGE_LOOP ( 'NONE', ( #117771, #92450, #91719, #78921 ) ) ;
#63542=DIRECTION ( 'NONE',  ( -0.7071067811865487940, 0.7071067811865463515, -0.000000000000000000 ) ) ;
#63543=AXIS2_PLACEMENT_3D ( 'NONE', #118581, #72985, #117141 ) ;
#63544=DIRECTION ( 'NONE',  ( 1.000000000000000000, 0.000000000000000000, 0.000000000000000000 ) ) ;
#63545=FACE_OUTER_BOUND ( 'NONE', #127036, .T. ) ;
#63546=ADVANCED_FACE ( 'NONE', ( #111773 ), #14593, .T. ) ;
#63547=ORIENTED_EDGE ( 'NONE', *, *, #89910, .T. ) ;
#63549=EDGE_LOOP ( 'NONE', ( #133610, #102562, #119437, #8603 ) ) ;
#63550=VECTOR ( 'NONE', #101428, 1000.000000000000000 ) ;
#63552=DIRECTION ( 'NONE',  ( 0.3543493200069162685, -0.000000000000000000, -0.9351131265310288487 ) ) ;
#63555=ORIENTED_EDGE ( 'NONE', *, *, #27513, .F. ) ;
#63556=LINE ( 'NONE', #66387, #69685 ) ;
#63557=CARTESIAN_POINT ( 'NONE',  ( 14.99999999999989697, 16.93112307739200872, 4.000000000000000000 ) ) ;
#63558=VECTOR ( 'NONE', #40641, 999.9999999999998863 ) ;
#63560=LINE ( 'NONE', #11244, #113389 ) ;
#63561=DIRECTION ( 'NONE',  ( -0.000000000000000000, -0.000000000000000000, 1.000000000000000000 ) ) ;
#63562=VERTEX_POINT ( 'NONE', #13848 ) ;
#63564=CARTESIAN_POINT ( 'NONE',  ( -1.786780966966399209, 12.75929247661558996, 10.29404684609034781 ) ) ;
#63565=LINE ( 'NONE', #88148, #23944 ) ;
#63566=CARTESIAN_POINT ( 'NONE',  ( -72.29974487139158157, -27.71228299555256669, 4.000000000000000000 ) ) ;
#63567=VECTOR ( 'NONE', #82022, 999.9999999999998863 ) ;
#63569=EDGE_CURVE ( 'NONE', #79010, #130681, #122629, .T. ) ;
#63570=ORIENTED_EDGE ( 'NONE', *, *, #32152, .T. ) ;
#63572=VECTOR ( 'NONE', #63988, 1000.000000000000000 ) ;
#63573=VECTOR ( 'NONE', #59388, 1000.000000000000227 ) ;
#63574=VERTEX_POINT ( 'NONE', #90750 ) ;
#63575=LINE ( 'NONE', #9857, #112445 ) ;
#63576=DIRECTION ( 'NONE',  ( 0.7071067811865486830, -0.7071067811865464625, -0.000000000000000000 ) ) ;
#63577=DIRECTION ( 'NONE',  ( -0.7071067811865487940, 0.7071067811865463515, 0.000000000000000000 ) ) ;
#63578=DIRECTION ( 'NONE',  ( -0.3543493200069162685, -0.000000000000000000, -0.9351131265310288487 ) ) ;
#63579=EDGE_LOOP ( 'NONE', ( #72370, #25613, #13566, #63643, #55989, #77099 ) ) ;
#63580=CARTESIAN_POINT ( 'NONE',  ( 57.18398860626899705, 28.73617430169827358, 5.000000000000000000 ) ) ;
#63581=FACE_OUTER_BOUND ( 'NONE', #22277, .T. ) ;
#63582=( BOUNDED_CURVE ( )  B_SPLINE_CURVE ( 3, ( #75345, #119505, #111518, #97787 ),
 .UNSPECIFIED., .F., .F. ) 
 B_SPLINE_CURVE_WITH_KNOTS ( ( 4, 4 ),
 ( 4.987589563512864643, 5.034563671340741564 ),
 .UNSPECIFIED. ) 
 CURVE ( )  GEOMETRIC_REPRESENTATION_ITEM ( )  RATIONAL_B_SPLINE_CURVE ( ( 1.000000000000000000, 0.9998161278856747547, 0.9998161278856747547, 1.000000000000000000 ) ) 
 REPRESENTATION_ITEM ( '' )  );
#63584=ORIENTED_EDGE ( 'NONE', *, *, #123462, .F. ) ;
#63585=ADVANCED_FACE ( 'NONE', ( #46562 ), #56721, .T. ) ;
#63587=CARTESIAN_POINT ( 'NONE',  ( 2.700255128608413990, -27.71228299555204089, 4.000000000000000000 ) ) ;
#63588=DIRECTION ( 'NONE',  ( 0.7071067811865486830, -0.7071067811865464625, -0.000000000000000000 ) ) ;
#63589=ORIENTED_EDGE ( 'NONE', *, *, #63060, .F. ) ;
#63590=VERTEX_POINT ( 'NONE', #44401 ) ;
#63592=LINE ( 'NONE', #108439, #100942 ) ;
#63593=CARTESIAN_POINT ( 'NONE',  ( 1.499999999999989120, -20.53675388469230256, 2.352720554255897323 ) ) ;
#63595=LINE ( 'NONE', #51981, #141634 ) ;
#63597=CARTESIAN_POINT ( 'NONE',  ( 0.000000000000000000, 0.000000000000000000, 5.000000000000000000 ) ) ;
#63599=VERTEX_POINT ( 'NONE', #113902 ) ;
#63600=VERTEX_POINT ( 'NONE', #57407 ) ;
#63601=ORIENTED_EDGE ( 'NONE', *, *, #113989, .T. ) ;
#63602=ORIENTED_EDGE ( 'NONE', *, *, #42750, .T. ) ;
#63605=DIRECTION ( 'NONE',  ( 1.000000000000000000, 0.000000000000000000, 0.000000000000000000 ) ) ;
#63606=PLANE ( 'NONE',  #63366 ) ;
#63607=EDGE_LOOP ( 'NONE', ( #34455, #7042, #10794, #73318 ) ) ;
#63608=FACE_OUTER_BOUND ( 'NONE', #126039, .T. ) ;
#63609=LINE ( 'NONE', #97613, #10168 ) ;
#63610=ADVANCED_FACE ( 'NONE', ( #66841 ), #55988, .T. ) ;
#63612=CARTESIAN_POINT ( 'NONE',  ( -4.171830600776436526, 0.7592924766157138627, 4.000000000000000000 ) ) ;
#63615=DIRECTION ( 'NONE',  ( 0.7071067811865487940, 0.7071067811865463515, 0.000000000000000000 ) ) ;
#63617=ORIENTED_EDGE ( 'NONE', *, *, #41052, .T. ) ;
#63618=EDGE_CURVE ( 'NONE', #112333, #122150, #132837, .T. ) ;
#63620=EDGE_LOOP ( 'NONE', ( #23859, #122785, #65580, #78257 ) ) ;
#63621=EDGE_CURVE ( 'NONE', #72549, #11328, #101588, .T. ) ;
#63622=ORIENTED_EDGE ( 'NONE', *, *, #34693, .F. ) ;
#63624=AXIS2_PLACEMENT_3D ( 'NONE', #30635, #73418, #74864 ) ;
#63625=EDGE_LOOP ( 'NONE', ( #70839, #68816, #1234, #103446 ) ) ;
#63626=ORIENTED_EDGE ( 'NONE', *, *, #26766, .F. ) ;
#63631=DIRECTION ( 'NONE',  ( -0.7071067811865486830, 0.7071067811865464625, 0.000000000000000000 ) ) ;
#63632=EDGE_CURVE ( 'NONE', #75329, #6181, #134978, .T. ) ;
#63635=CARTESIAN_POINT ( 'NONE',  ( 5.999999999999956479, -2.904428200921311376, -6.989807076074958658 ) ) ;
#63636=DIRECTION ( 'NONE',  ( 1.000000000000000000, 0.000000000000000000, 0.000000000000000000 ) ) ;
#63637=EDGE_CURVE ( 'NONE', #26091, #101520, #45819, .T. ) ;
#63638=LINE ( 'NONE', #73767, #16692 ) ;
#63640=ORIENTED_EDGE ( 'NONE', *, *, #40724, .T. ) ;
#63641=PLANE ( 'NONE',  #80499 ) ;
#63642=ORIENTED_EDGE ( 'NONE', *, *, #9571, .T. ) ;
#63643=ORIENTED_EDGE ( 'NONE', *, *, #30784, .F. ) ;
#63644=ORIENTED_EDGE ( 'NONE', *, *, #138169, .F. ) ;
#63645=VERTEX_POINT ( 'NONE', #102341 ) ;
#63647=DIRECTION ( 'NONE',  ( 0.7071067811865487940, -0.7071067811865463515, 0.000000000000000000 ) ) ;
#63649=ORIENTED_EDGE ( 'NONE', *, *, #71392, .T. ) ;
#63651=VERTEX_POINT ( 'NONE', #111020 ) ;
#63654=LINE ( 'NONE', #20098, #4437 ) ;
#63655=EDGE_CURVE ( 'NONE', #42001, #103370, #91455, .T. ) ;
#63656=CARTESIAN_POINT ( 'NONE',  ( -13.01987774928539032, -17.24070752338409918, 20.23474786156466010 ) ) ;
#63657=AXIS2_PLACEMENT_3D ( 'NONE', #64291, #98355, #107766 ) ;
#63658=CARTESIAN_POINT ( 'NONE',  ( 22.49999999999984368, 9.431123077392088661, 4.000000000000000000 ) ) ;
#63659=ORIENTED_EDGE ( 'NONE', *, *, #18605, .F. ) ;
#63660=ADVANCED_FACE ( 'NONE', ( #113173 ), #133527, .F. ) ;
#63661=EDGE_LOOP ( 'NONE', ( #54877, #11093, #45083, #22574 ) ) ;
#63662=EDGE_LOOP ( 'NONE', ( #138564, #23991, #96097, #91239 ) ) ;
#63663=DIRECTION ( 'NONE',  ( -1.000000000000000000, 0.000000000000000000, -0.000000000000000000 ) ) ;
#63664=LINE ( 'NONE', #107824, #48812 ) ;
#63665=CARTESIAN_POINT ( 'NONE',  ( -14.20666063542142687, 21.75929247661549937, 4.998822639870708073 ) ) ;
#63667=EDGE_CURVE ( 'NONE', #137445, #133889, #134244, .T. ) ;
#63668=ADVANCED_FACE ( 'NONE', ( #34937 ), #836, .F. ) ;
#63669=DIRECTION ( 'NONE',  ( -1.000000000000000000, 0.000000000000000000, 0.000000000000000000 ) ) ;
#63672=CARTESIAN_POINT ( 'NONE',  ( 8.536408254699722420, -22.22500000000000142, 21.46915226046162672 ) ) ;
#63673=LINE ( 'NONE', #107832, #58228 ) ;
#63674=ORIENTED_EDGE ( 'NONE', *, *, #5307, .T. ) ;
#63675=CARTESIAN_POINT ( 'NONE',  ( 15.29974487139158867, -27.71228299555216879, 4.000000000000000000 ) ) ;
#63676=CARTESIAN_POINT ( 'NONE',  ( -17.99999999999987566, 14.87792677143806941, -11.06722581663444060 ) ) ;
#63677=EDGE_LOOP ( 'NONE', ( #12412, #70061, #5024, #641, #51113, #61732 ) ) ;
#63678=DIRECTION ( 'NONE',  ( 0.7071067811865486830, -0.7071067811865464625, -0.000000000000000000 ) ) ;
#63680=VERTEX_POINT ( 'NONE', #13137 ) ;
#63681=EDGE_CURVE ( 'NONE', #102321, #63466, #2250, .T. ) ;
#63682=EDGE_CURVE ( 'NONE', #70988, #7787, #73277, .T. ) ;
#63683=CARTESIAN_POINT ( 'NONE',  ( 3.489213562373097322, -27.52281430457057709, 5.000000000000000000 ) ) ;
#63684=VERTEX_POINT ( 'NONE', #70456 ) ;
#63687=DIRECTION ( 'NONE',  ( -0.3543493200069163240, 0.000000000000000000, 0.9351131265310288487 ) ) ;
#63691=FACE_OUTER_BOUND ( 'NONE', #8635, .T. ) ;
#63693=FACE_OUTER_BOUND ( 'NONE', #33031, .T. ) ;
#63695=CARTESIAN_POINT ( 'NONE',  ( -32.48334561358932149, 22.22500000000000142, 4.500000000000000888 ) ) ;
#63698=EDGE_CURVE ( 'NONE', #35574, #18121, #3674, .T. ) ;
#63699=DIRECTION ( 'NONE',  ( -0.6830127018922180770, -0.6830127018922204085, -0.2588190451025213501 ) ) ;
#63700=CARTESIAN_POINT ( 'NONE',  ( 13.35824297541131322, 15.75929247661555088, 19.34181609438696370 ) ) ;
#63701=VERTEX_POINT ( 'NONE', #61694 ) ;
#63702=ORIENTED_EDGE ( 'NONE', *, *, #73931, .T. ) ;
#63703=LINE ( 'NONE', #116630, #28095 ) ;
#63704=VERTEX_POINT ( 'NONE', #26193 ) ;
#63705=LINE ( 'NONE', #41942, #133643 ) ;
#63706=DIRECTION ( 'NONE',  ( -0.000000000000000000, 0.000000000000000000, 1.000000000000000000 ) ) ;
#63707=CARTESIAN_POINT ( 'NONE',  ( -48.48921356237309510, -27.52281430457089328, 5.000000000000000000 ) ) ;
#63708=EDGE_CURVE ( 'NONE', #132084, #47759, #15974, .T. ) ;
#63710=CARTESIAN_POINT ( 'NONE',  ( 10.82816939922345156, -11.24070752338417201, 4.000000000000000000 ) ) ;
#63711=DIRECTION ( 'NONE',  ( 0.7071067811865487940, -0.7071067811865463515, 0.000000000000000000 ) ) ;
#63712=CARTESIAN_POINT ( 'NONE',  ( -3.299744871391591339, -27.71228299555208352, 4.000000000000000000 ) ) ;
#63714=CARTESIAN_POINT ( 'NONE',  ( -63.48921356237309510, -27.52281430457099631, 5.000000000000000000 ) ) ;
#63715=ORIENTED_EDGE ( 'NONE', *, *, #75503, .F. ) ;
#63716=CARTESIAN_POINT ( 'NONE',  ( -51.18398860626899705, 28.73617430169823095, 5.000000000000000000 ) ) ;
#63717=ADVANCED_FACE ( 'NONE', ( #61006 ), #103709, .F. ) ;
#63719=DIRECTION ( 'NONE',  ( -0.7071067811865487940, 0.7071067811865463515, -0.000000000000000000 ) ) ;
#63720=CARTESIAN_POINT ( 'NONE',  ( 45.18398860626900415, 28.73617430169818832, 5.000000000000000000 ) ) ;
#63721=DIRECTION ( 'NONE',  ( 0.3543493200069162685, -0.000000000000000000, -0.9351131265310288487 ) ) ;
#63722=ORIENTED_EDGE ( 'NONE', *, *, #90073, .T. ) ;
#63724=VECTOR ( 'NONE', #73167, 1000.000000000000000 ) ;
#63725=ORIENTED_EDGE ( 'NONE', *, *, #70898, .T. ) ;
#63726=ORIENTED_EDGE ( 'NONE', *, *, #135209, .F. ) ;
#63728=( BOUNDED_CURVE ( )  B_SPLINE_CURVE ( 3, ( #112803, #91085, #55596, #112116 ),
 .UNSPECIFIED., .F., .T. ) 
 B_SPLINE_CURVE_WITH_KNOTS ( ( 4, 4 ),
 ( 1.208578181583236821, 1.359146454359400957 ),
 .UNSPECIFIED. ) 
 CURVE ( )  GEOMETRIC_REPRESENTATION_ITEM ( )  RATIONAL_B_SPLINE_CURVE ( ( 1.000000000000000000, 0.9981116584018963067, 0.9981116584018963067, 1.000000000000000000 ) ) 
 REPRESENTATION_ITEM ( '' )  );
#63729=ORIENTED_EDGE ( 'NONE', *, *, #19130, .T. ) ;
#63730=VECTOR ( 'NONE', #127357, 1000.000000000000000 ) ;
#63732=DIRECTION ( 'NONE',  ( 0.7071067811865486830, -0.7071067811865464625, -0.000000000000000000 ) ) ;
#63733=ORIENTED_EDGE ( 'NONE', *, *, #32704, .F. ) ;
#63738=VECTOR ( 'NONE', #67428, 1000.000000000000000 ) ;
#63740=CARTESIAN_POINT ( 'NONE',  ( 54.18398860626899705, 28.73617430169825226, 5.000000000000000000 ) ) ;
#63741=CARTESIAN_POINT ( 'NONE',  ( -33.48921356237309510, -27.52281430457078670, 5.000000000000000000 ) ) ;
#63742=CARTESIAN_POINT ( 'NONE',  ( 2.488313940715670913, 6.759292476615645917, 16.35960578974468760 ) ) ;
#63743=CARTESIAN_POINT ( 'NONE',  ( 8.292893218813404133, 14.25929247661557753, 5.000000000000000000 ) ) ;
#63744=VERTEX_POINT ( 'NONE', #139967 ) ;
#63745=ORIENTED_EDGE ( 'NONE', *, *, #10334, .T. ) ;
#63746=ORIENTED_EDGE ( 'NONE', *, *, #11344, .T. ) ;
#63747=LINE ( 'NONE', #107218, #19075 ) ;
#63748=CARTESIAN_POINT ( 'NONE',  ( 6.489213562373093325, -27.52281430457059841, 5.000000000000000000 ) ) ;
#63749=LINE ( 'NONE', #8576, #135940 ) ;
#63752=VECTOR ( 'NONE', #125852, 1000.000000000000000 ) ;
#63753=VECTOR ( 'NONE', #18007, 1000.000000000000000 ) ;
#63754=ORIENTED_EDGE ( 'NONE', *, *, #78212, .F. ) ;
#63755=ORIENTED_EDGE ( 'NONE', *, *, #86620, .T. ) ;
#63757=EDGE_LOOP ( 'NONE', ( #96513, #132186, #85429, #2075 ) ) ;
#63758=EDGE_CURVE ( 'NONE', #120820, #11462, #8660, .T. ) ;
#63759=ADVANCED_FACE ( 'NONE', ( #75410 ), #129771, .F. ) ;
#63760=EDGE_LOOP ( 'NONE', ( #56059, #17555, #32575, #87002 ) ) ;
#63761=CARTESIAN_POINT ( 'NONE',  ( 0.000000000000000000, 0.000000000000000000, 5.000000000000000000 ) ) ;
#63762=CARTESIAN_POINT ( 'NONE',  ( -14.99999999999989164, 19.55218569542897100, 5.000000000000000000 ) ) ;
#63763=ORIENTED_EDGE ( 'NONE', *, *, #64654, .T. ) ;
#63764=LINE ( 'NONE', #54333, #129296 ) ;
#63766=CARTESIAN_POINT ( 'NONE',  ( -34.42500000000001137, 0.000000000000000000, 4.500000000000000888 ) ) ;
#63768=CARTESIAN_POINT ( 'NONE',  ( 28.49999999999980460, -10.53360074219763121, 5.000000000000000000 ) ) ;
#63769=VERTEX_POINT ( 'NONE', #10132 ) ;
#63772=ORIENTED_EDGE ( 'NONE', *, *, #50333, .F. ) ;
#63773=CARTESIAN_POINT ( 'NONE',  ( -17.99451991528748351, 28.92564299267950645, 4.000000000000000000 ) ) ;
#63774=EDGE_CURVE ( 'NONE', #93762, #97422, #142108, .T. ) ;
#63776=ORIENTED_EDGE ( 'NONE', *, *, #90851, .F. ) ;
#63778=VERTEX_POINT ( 'NONE', #107989 ) ;
#63779=LINE ( 'NONE', #107937, #110658 ) ;
#63781=VERTEX_POINT ( 'NONE', #118154 ) ;
#63782=ORIENTED_EDGE ( 'NONE', *, *, #123667, .F. ) ;
#63783=ORIENTED_EDGE ( 'NONE', *, *, #100311, .T. ) ;
#63784=EDGE_CURVE ( 'NONE', #113425, #34606, #42794, .T. ) ;
#63787=CARTESIAN_POINT ( 'NONE',  ( 27.18398860626900060, 28.73617430169806042, 5.000000000000000000 ) ) ;
#63789=CARTESIAN_POINT ( 'NONE',  ( 51.48921356237309510, -27.52281430457091460, 5.000000000000000000 ) ) ;
#63790=ADVANCED_FACE ( 'NONE', ( #131935 ), #32627, .F. ) ;
#63791=CARTESIAN_POINT ( 'NONE',  ( 24.48921356237309510, -27.52281430457072631, 5.000000000000000000 ) ) ;
#63792=CARTESIAN_POINT ( 'NONE',  ( -59.99451991528749772, 28.92564299267980132, 4.000000000000000000 ) ) ;
#63793=PLANE ( 'NONE',  #16735 ) ;
#63795=DIRECTION ( 'NONE',  ( 0.7071067811865487940, 0.7071067811865463515, 0.000000000000000000 ) ) ;
#63796=CARTESIAN_POINT ( 'NONE',  ( -54.29974487139159578, -27.71228299555243879, 4.000000000000000000 ) ) ;
#63797=CARTESIAN_POINT ( 'NONE',  ( -30.31657961132771462, -6.740707523384216415, 11.88629033278131253 ) ) ;
#63799=VERTEX_POINT ( 'NONE', #40643 ) ;
#63801=ORIENTED_EDGE ( 'NONE', *, *, #11960, .T. ) ;
#63802=CARTESIAN_POINT ( 'NONE',  ( 35.99451991528749772, 28.92564299267963079, 4.000000000000000000 ) ) ;
#63803=EDGE_CURVE ( 'NONE', #55828, #10662, #54394, .T. ) ;
#63804=VERTEX_POINT ( 'NONE', #76117 ) ;
#63805=ORIENTED_EDGE ( 'NONE', *, *, #59669, .F. ) ;
#63808=LINE ( 'NONE', #118875, #127336 ) ;
#63809=VERTEX_POINT ( 'NONE', #76858 ) ;
#63810=DIRECTION ( 'NONE',  ( 0.7071067811865487940, 0.7071067811865463515, 0.000000000000000000 ) ) ;
#63811=EDGE_CURVE ( 'NONE', #29477, #17037, #71806, .T. ) ;
#63812=VERTEX_POINT ( 'NONE', #130514 ) ;
#63813=AXIS2_PLACEMENT_3D ( 'NONE', #128611, #29286, #83714 ) ;
#63814=CARTESIAN_POINT ( 'NONE',  ( 27.29974487139158512, -27.71228299555225405, 4.000000000000000000 ) ) ;
#63816=ORIENTED_EDGE ( 'NONE', *, *, #1520, .T. ) ;
#63819=CARTESIAN_POINT ( 'NONE',  ( -41.99451991528749062, 28.92564299267967343, 4.000000000000000000 ) ) ;
#63820=CARTESIAN_POINT ( 'NONE',  ( -48.48921356237309510, -27.52281430457089328, 5.000000000000000000 ) ) ;
#63822=EDGE_CURVE ( 'NONE', #74472, #104351, #31193, .T. ) ;
#63823=ORIENTED_EDGE ( 'NONE', *, *, #12871, .T. ) ;
#63824=DIRECTION ( 'NONE',  ( -0.6830127018922181881, 0.6830127018922202975, -0.2588190451025214056 ) ) ;
#63825=ORIENTED_EDGE ( 'NONE', *, *, #66618, .T. ) ;
#63826=DIRECTION ( 'NONE',  ( 0.6830127018922181881, 0.6830127018922202975, -0.2588190451025214056 ) ) ;
#63828=PLANE ( 'NONE',  #58573 ) ;
#63829=CARTESIAN_POINT ( 'NONE',  ( -34.92500000000001137, 22.22500000000000142, 4.000000000000000000 ) ) ;
#63830=ORIENTED_EDGE ( 'NONE', *, *, #121619, .F. ) ;
#63831=EDGE_CURVE ( 'NONE', #133340, #109375, #41324, .T. ) ;
#63832=EDGE_CURVE ( 'NONE', #132213, #115620, #21003, .T. ) ;
#63835=CARTESIAN_POINT ( 'NONE',  ( -8.999999999999944933, 14.58746187583910903, 4.000000000000000000 ) ) ;
#63836=DIRECTION ( 'NONE',  ( 0.7071067811865486830, -0.7071067811865464625, -0.000000000000000000 ) ) ;
#63838=DIRECTION ( 'NONE',  ( 0.7071067811865486830, -0.7071067811865464625, -0.000000000000000000 ) ) ;
#63839=PLANE ( 'NONE',  #121106 ) ;
#63840=ADVANCED_FACE ( 'NONE', ( #129053 ), #109449, .F. ) ;
#63842=CARTESIAN_POINT ( 'NONE',  ( -1.499999999999986677, -16.53360074219757792, 5.000000000000000000 ) ) ;
#63843=ORIENTED_EDGE ( 'NONE', *, *, #32136, .T. ) ;
#63844=EDGE_CURVE ( 'NONE', #100802, #55039, #63126, .T. ) ;
#63845=ORIENTED_EDGE ( 'NONE', *, *, #11005, .F. ) ;
#63846=CARTESIAN_POINT ( 'NONE',  ( -8.999999999999925393, -22.06887692260758982, 4.000000000000000000 ) ) ;
#63848=ORIENTED_EDGE ( 'NONE', *, *, #86125, .F. ) ;
#63849=DIRECTION ( 'NONE',  ( 0.7071067811865487940, 0.7071067811865463515, -0.000000000000000000 ) ) ;
#63853=VECTOR ( 'NONE', #26279, 1000.000000000000114 ) ;
#63855=VECTOR ( 'NONE', #101579, 1000.000000000000000 ) ;
#63856=ADVANCED_FACE ( 'NONE', ( #47113 ), #80418, .F. ) ;
#63857=CARTESIAN_POINT ( 'NONE',  ( 34.92499999999998295, 22.22500000000000142, 4.000000000000000000 ) ) ;
#63859=DIRECTION ( 'NONE',  ( -0.7071067811865486830, -0.7071067811865464625, 0.000000000000000000 ) ) ;
#63860=DIRECTION ( 'NONE',  ( 0.7071067811865487940, 0.7071067811865463515, -0.000000000000000000 ) ) ;
#63861=CARTESIAN_POINT ( 'NONE',  ( 1.500000000000001332, 10.46639925780216274, 5.000000000000000000 ) ) ;
#63862=CARTESIAN_POINT ( 'NONE',  ( 17.51078643762690845, -27.52281430457043143, 5.000000000000000000 ) ) ;
#63863=DIRECTION ( 'NONE',  ( -0.6830127018922180770, -0.6830127018922204085, -0.2588190451025213501 ) ) ;
#63865=EDGE_CURVE ( 'NONE', #39389, #106040, #135505, .T. ) ;
#63869=ORIENTED_EDGE ( 'NONE', *, *, #105018, .T. ) ;
#63870=ORIENTED_EDGE ( 'NONE', *, *, #23922, .F. ) ;
#63872=ORIENTED_EDGE ( 'NONE', *, *, #141699, .F. ) ;
#63873=ORIENTED_EDGE ( 'NONE', *, *, #4009, .F. ) ;
#63874=ORIENTED_EDGE ( 'NONE', *, *, #96654, .F. ) ;
#63875=DIRECTION ( 'NONE',  ( 0.6830127018922180770, -0.6830127018922204085, -0.2588190451025213501 ) ) ;
#63876=LINE ( 'NONE', #31244, #129626 ) ;
#63877=EDGE_LOOP ( 'NONE', ( #76794, #35866, #86838, #93543 ) ) ;
#63879=PLANE ( 'NONE',  #4598 ) ;
#63880=DIRECTION ( 'NONE',  ( -0.000000000000000000, 0.000000000000000000, 1.000000000000000000 ) ) ;
#63883=ORIENTED_EDGE ( 'NONE', *, *, #50517, .F. ) ;
#63884=PLANE ( 'NONE',  #106652 ) ;
#63885=CARTESIAN_POINT ( 'NONE',  ( 51.48921356237309510, -27.52281430457091460, 5.000000000000000000 ) ) ;
#63886=DIRECTION ( 'NONE',  ( 1.000000000000000000, 0.000000000000000000, 0.000000000000000000 ) ) ;
#63887=CARTESIAN_POINT ( 'NONE',  ( -31.49999999999977973, 15.05218569542901186, 5.000000000000000000 ) ) ;
#63888=DIRECTION ( 'NONE',  ( -0.7071067811865486830, -0.7071067811865464625, 0.000000000000000000 ) ) ;
#63889=LINE ( 'NONE', #108051, #73182 ) ;
#63891=CARTESIAN_POINT ( 'NONE',  ( -4.499999999999962697, -19.53360074219753884, 5.000000000000000000 ) ) ;
#63892=ORIENTED_EDGE ( 'NONE', *, *, #117157, .T. ) ;
#63895=VERTEX_POINT ( 'NONE', #36189 ) ;
#63896=FACE_OUTER_BOUND ( 'NONE', #1853, .T. ) ;
#63897=PLANE ( 'NONE',  #114947 ) ;
#63898=FACE_OUTER_BOUND ( 'NONE', #24915, .T. ) ;
#63899=CARTESIAN_POINT ( 'NONE',  ( 10.49999999999993250, 13.46639925780212366, 5.000000000000000000 ) ) ;
#63900=DIRECTION ( 'NONE',  ( 0.7071067811865487940, 0.7071067811865463515, -0.000000000000000000 ) ) ;
#63901=CARTESIAN_POINT ( 'NONE',  ( 2.999999999999975131, -16.02097659208071079, -11.96015758381209082 ) ) ;
#63903=ORIENTED_EDGE ( 'NONE', *, *, #10075, .F. ) ;
#63904=FACE_OUTER_BOUND ( 'NONE', #125372, .T. ) ;
#63905=ORIENTED_EDGE ( 'NONE', *, *, #55768, .T. ) ;
#63906=FACE_OUTER_BOUND ( 'NONE', #94280, .T. ) ;
#63909=CARTESIAN_POINT ( 'NONE',  ( 17.99999999999987210, 15.45873954670186734, -0.03131636524298340996 ) ) ;
#63910=VERTEX_POINT ( 'NONE', #55811 ) ;
#63912=ORIENTED_EDGE ( 'NONE', *, *, #100029, .F. ) ;
#63913=CARTESIAN_POINT ( 'NONE',  ( -18.69326993309588403, -3.740707523384244837, 12.88036043432871836 ) ) ;
#63914=CARTESIAN_POINT ( 'NONE',  ( 32.35681257248241849, -20.24070752338406720, 21.22881796311220270 ) ) ;
#63915=DIRECTION ( 'NONE',  ( -0.6830127018922181881, 0.6830127018922202975, -0.2588190451025214056 ) ) ;
#63916=VECTOR ( 'NONE', #5008, 1000.000000000000000 ) ;
#63918=ORIENTED_EDGE ( 'NONE', *, *, #130762, .T. ) ;
#63919=VECTOR ( 'NONE', #7163, 1000.000000000000000 ) ;
#63921=EDGE_LOOP ( 'NONE', ( #64878, #101212, #23979, #104177 ) ) ;
#63922=VERTEX_POINT ( 'NONE', #132676 ) ;
#63923=VERTEX_POINT ( 'NONE', #21735 ) ;
#63924=ADVANCED_FACE ( 'NONE', ( #102163 ), #100012, .F. ) ;
#63926=DIRECTION ( 'NONE',  ( 0.7071067811865487940, 0.7071067811865463515, 0.000000000000000000 ) ) ;
#63927=ORIENTED_EDGE ( 'NONE', *, *, #22321, .T. ) ;
#63928=CARTESIAN_POINT ( 'NONE',  ( 29.29289321881325847, -3.740707523384241728, 5.000000000000000000 ) ) ;
#63930=CARTESIAN_POINT ( 'NONE',  ( 17.99999999999987566, 16.55218569542899587, 5.000000000000000000 ) ) ;
#63931=CARTESIAN_POINT ( 'NONE',  ( 48.48921356237309510, -27.52281430457089328, 5.000000000000000000 ) ) ;
#63932=ADVANCED_FACE ( 'NONE', ( #113005 ), #11530, .T. ) ;
#63933=FACE_BOUND ( 'NONE', #123471, .T. ) ;
#63934=ORIENTED_EDGE ( 'NONE', *, *, #51160, .T. ) ;
#63935=EDGE_CURVE ( 'NONE', #137150, #122980, #22412, .T. ) ;
#63937=LINE ( 'NONE', #31308, #53774 ) ;
#63938=CARTESIAN_POINT ( 'NONE',  ( -50.99451991528749062, 28.92564299267973738, 4.000000000000000000 ) ) ;
#63939=ORIENTED_EDGE ( 'NONE', *, *, #42904, .F. ) ;
#63940=ORIENTED_EDGE ( 'NONE', *, *, #76754, .F. ) ;
#63941=ORIENTED_EDGE ( 'NONE', *, *, #99841, .F. ) ;
#63943=VECTOR ( 'NONE', #127001, 1000.000000000000227 ) ;
#63945=ADVANCED_FACE ( 'NONE', ( #133364 ), #100726, .F. ) ;
#63947=VECTOR ( 'NONE', #9661, 1000.000000000000227 ) ;
#63950=DIRECTION ( 'NONE',  ( -0.000000000000000000, 0.000000000000000000, 1.000000000000000000 ) ) ;
#63951=DIRECTION ( 'NONE',  ( 0.7071067811865487940, 0.7071067811865463515, 0.000000000000000000 ) ) ;
#63952=EDGE_CURVE ( 'NONE', #139559, #86675, #12271, .T. ) ;
#63953=VERTEX_POINT ( 'NONE', #55085 ) ;
#63955=LINE ( 'NONE', #131343, #20372 ) ;
#63957=EDGE_CURVE ( 'NONE', #114197, #108193, #99256, .T. ) ;
#63959=CARTESIAN_POINT ( 'NONE',  ( -72.18398860626899705, 28.73617430169837661, 5.000000000000000000 ) ) ;
#63960=CARTESIAN_POINT ( 'NONE',  ( 22.49999999999985434, 22.08746187583901843, 4.000000000000000000 ) ) ;
#63961=CARTESIAN_POINT ( 'NONE',  ( -81.18398860626899705, 28.73617430169844056, 5.000000000000000000 ) ) ;
#63962=DIRECTION ( 'NONE',  ( -0.000000000000000000, 0.000000000000000000, 1.000000000000000000 ) ) ;
#63963=ORIENTED_EDGE ( 'NONE', *, *, #131077, .T. ) ;
#63964=EDGE_CURVE ( 'NONE', #50789, #140166, #44220, .T. ) ;
#63966=PLANE ( 'NONE',  #79143 ) ;
#63967=EDGE_LOOP ( 'NONE', ( #71136, #80870, #82059, #35051 ) ) ;
#63968=ORIENTED_EDGE ( 'NONE', *, *, #19393, .T. ) ;
#63970=CARTESIAN_POINT ( 'NONE',  ( 5.010880286539447503, -22.02621442084248926, 4.990779571109220214 ) ) ;
#63971=CARTESIAN_POINT ( 'NONE',  ( -2.999999999999975131, 9.631307414974321190, -9.079085613539549016 ) ) ;
#63972=PLANE ( 'NONE',  #9111 ) ;
#63973=EDGE_LOOP ( 'NONE', ( #30423, #460, #29367 ) ) ;
#63975=ADVANCED_FACE ( 'NONE', ( #143500 ), #45658, .F. ) ;
#63976=DIRECTION ( 'NONE',  ( 0.7071067811865487940, 0.7071067811865463515, 0.000000000000000000 ) ) ;
#63978=ORIENTED_EDGE ( 'NONE', *, *, #97203, .F. ) ;
#63980=CARTESIAN_POINT ( 'NONE',  ( -5.700255128608413102, -27.71228299555201957, 4.000000000000000000 ) ) ;
#63982=DIRECTION ( 'NONE',  ( 0.6830127018922180770, -0.6830127018922204085, -0.2588190451025213501 ) ) ;
#63983=DIRECTION ( 'NONE',  ( 0.7071067811865487940, 0.7071067811865463515, 0.000000000000000000 ) ) ;
#63985=VECTOR ( 'NONE', #53340, 1000.000000000000000 ) ;
#63987=ORIENTED_EDGE ( 'NONE', *, *, #34863, .T. ) ;
#63988=DIRECTION ( 'NONE',  ( 0.7071067811865486830, -0.7071067811865464625, -0.000000000000000000 ) ) ;
#63989=DIRECTION ( 'NONE',  ( -1.000000000000000000, 0.000000000000000000, -0.000000000000000000 ) ) ;
#63991=ORIENTED_EDGE ( 'NONE', *, *, #131385, .F. ) ;
#63992=EDGE_CURVE ( 'NONE', #31310, #119557, #46385, .T. ) ;
#63993=ADVANCED_FACE ( 'NONE', ( #110839 ), #123206, .F. ) ;
#63994=DIRECTION ( 'NONE',  ( 0.7071067811865487940, 0.7071067811865463515, 0.000000000000000000 ) ) ;
#63996=AXIS2_PLACEMENT_3D ( 'NONE', #38014, #51736, #39438 ) ;
#63997=ORIENTED_EDGE ( 'NONE', *, *, #54093, .T. ) ;
#63998=DIRECTION ( 'NONE',  ( -0.000000000000000000, -0.3543493200069152693, 0.9351131265310292928 ) ) ;
#63999=( BOUNDED_CURVE ( )  B_SPLINE_CURVE ( 3, ( #122773, #101015, #132979, #90892 ),
 .UNSPECIFIED., .F., .T. ) 
 B_SPLINE_CURVE_WITH_KNOTS ( ( 4, 4 ),
 ( 1.864375635226923400, 1.933014472006560958 ),
 .UNSPECIFIED. ) 
 CURVE ( )  GEOMETRIC_REPRESENTATION_ITEM ( )  RATIONAL_B_SPLINE_CURVE ( ( 1.000000000000000000, 0.9996074310407762065, 0.9996074310407762065, 1.000000000000000000 ) ) 
 REPRESENTATION_ITEM ( '' )  );
#64001=EDGE_CURVE ( 'NONE', #58035, #45698, #91974, .T. ) ;
#64003=CARTESIAN_POINT ( 'NONE',  ( -34.42500000000001137, 8.977185695429334089, 5.000000000000000000 ) ) ;
#64005=ORIENTED_EDGE ( 'NONE', *, *, #71864, .F. ) ;
#64006=ORIENTED_EDGE ( 'NONE', *, *, #20255, .T. ) ;
#64008=CARTESIAN_POINT ( 'NONE',  ( -10.82816939922345156, 21.75929247661549937, 4.000000000000000000 ) ) ;
#64011=VECTOR ( 'NONE', #133144, 1000.000000000000227 ) ;
#64013=DIRECTION ( 'NONE',  ( -0.7071067811865486830, -0.7071067811865464625, -0.000000000000000000 ) ) ;
#64016=ORIENTED_EDGE ( 'NONE', *, *, #118453, .T. ) ;
#64017=EDGE_CURVE ( 'NONE', #112008, #56955, #113733, .T. ) ;
#64018=DIRECTION ( 'NONE',  ( 1.000000000000000000, 0.000000000000000000, 0.000000000000000000 ) ) ;
#64019=DIRECTION ( 'NONE',  ( 0.6830127018922181881, 0.6830127018922202975, -0.2588190451025214056 ) ) ;
#64020=CARTESIAN_POINT ( 'NONE',  ( 33.18398860626899705, 28.73617430169810305, 5.000000000000000000 ) ) ;
#64021=LINE ( 'NONE', #53112, #18197 ) ;
#64023=CARTESIAN_POINT ( 'NONE',  ( 32.29298673570672662, -21.74070752338405654, 4.999753212805222446 ) ) ;
#64024=ORIENTED_EDGE ( 'NONE', *, *, #129111, .F. ) ;
#64025=CARTESIAN_POINT ( 'NONE',  ( -30.32816939922331656, -15.74070752338412760, 4.000000000000000000 ) ) ;
#64026=EDGE_LOOP ( 'NONE', ( #139510, #138511, #31746, #45888 ) ) ;
#64027=VECTOR ( 'NONE', #24346, 1000.000000000000000 ) ;
#64028=VERTEX_POINT ( 'NONE', #103543 ) ;
#64029=LINE ( 'NONE', #108197, #31702 ) ;
#64030=LINE ( 'NONE', #11028, #34760 ) ;
#64031=ORIENTED_EDGE ( 'NONE', *, *, #73436, .T. ) ;
#64033=CARTESIAN_POINT ( 'NONE',  ( -24.18398860626899705, 28.73617430169804265, 5.000000000000000000 ) ) ;
#64034=DIRECTION ( 'NONE',  ( 0.000000000000000000, 1.000000000000000000, 0.000000000000000000 ) ) ;
#64035=EDGE_CURVE ( 'NONE', #49314, #39393, #26017, .T. ) ;
#64036=VECTOR ( 'NONE', #70711, 1000.000000000000000 ) ;
#64038=CARTESIAN_POINT ( 'NONE',  ( -30.29974487139158867, -27.71228299555227537, 4.000000000000000000 ) ) ;
#64039=ORIENTED_EDGE ( 'NONE', *, *, #50510, .T. ) ;
#64040=DIRECTION ( 'NONE',  ( -0.000000000000000000, -0.3543493200069152693, 0.9351131265310292928 ) ) ;
#64041=DIRECTION ( 'NONE',  ( 0.7071067811865487940, 0.7071067811865463515, 0.000000000000000000 ) ) ;
#64042=LINE ( 'NONE', #140857, #107463 ) ;
#64044=CARTESIAN_POINT ( 'NONE',  ( 29.27718569542920335, -21.72500000000000142, 5.000000000000000000 ) ) ;
#64045=AXIS2_PLACEMENT_3D ( 'NONE', #62135, #138982, #128110 ) ;
#64048=VECTOR ( 'NONE', #142879, 1000.000000000000000 ) ;
#64049=FACE_OUTER_BOUND ( 'NONE', #7387, .T. ) ;
#64051=ORIENTED_EDGE ( 'NONE', *, *, #43557, .F. ) ;
#64053=DIRECTION ( 'NONE',  ( 0.7071067811865486830, -0.7071067811865464625, -0.000000000000000000 ) ) ;
#64054=CARTESIAN_POINT ( 'NONE',  ( 6.183988606268994381, 28.73617430169791476, 5.000000000000000000 ) ) ;
#64055=VECTOR ( 'NONE', #51383, 1000.000000000000000 ) ;
#64056=LINE ( 'NONE', #61934, #11319 ) ;
#64057=VERTEX_POINT ( 'NONE', #92673 ) ;
#64058=DIRECTION ( 'NONE',  ( -0.000000000000000000, -0.000000000000000000, 1.000000000000000000 ) ) ;
#64059=EDGE_CURVE ( 'NONE', #125931, #66092, #49216, .T. ) ;
#64061=ORIENTED_EDGE ( 'NONE', *, *, #42924, .F. ) ;
#64062=CARTESIAN_POINT ( 'NONE',  ( 34.49999999999975842, -10.53574439159940113, 4.994342998332163219 ) ) ;
#64063=VERTEX_POINT ( 'NONE', #102872 ) ;
#64064=EDGE_LOOP ( 'NONE', ( #63825, #99845, #16428, #51301 ) ) ;
#64067=DIRECTION ( 'NONE',  ( -0.7071067811865486830, -0.7071067811865464625, 0.000000000000000000 ) ) ;
#64069=ORIENTED_EDGE ( 'NONE', *, *, #131227, .F. ) ;
#64070=EDGE_CURVE ( 'NONE', #35249, #127932, #104987, .T. ) ;
#64071=PLANE ( 'NONE',  #113703 ) ;
#64072=LINE ( 'NONE', #32900, #119341 ) ;
#64073=ORIENTED_EDGE ( 'NONE', *, *, #65647, .F. ) ;
#64076=FACE_OUTER_BOUND ( 'NONE', #62304, .T. ) ;
#64077=DIRECTION ( 'NONE',  ( -0.000000000000000000, -0.000000000000000000, 1.000000000000000000 ) ) ;
#64078=VERTEX_POINT ( 'NONE', #27413 ) ;
#64079=VECTOR ( 'NONE', #99991, 999.9999999999998863 ) ;
#64080=FACE_OUTER_BOUND ( 'NONE', #82834, .T. ) ;
#64082=FACE_OUTER_BOUND ( 'NONE', #44192, .T. ) ;
#64083=LINE ( 'NONE', #51074, #87117 ) ;
#64084=LINE ( 'NONE', #8234, #131183 ) ;
#64085=ORIENTED_EDGE ( 'NONE', *, *, #17529, .F. ) ;
#64086=ORIENTED_EDGE ( 'NONE', *, *, #60920, .T. ) ;
#64087=AXIS2_PLACEMENT_3D ( 'NONE', #17509, #95065, #59630 ) ;
#64088=CARTESIAN_POINT ( 'NONE',  ( -60.18398860626900415, 28.73617430169829490, 5.000000000000000000 ) ) ;
#64090=VERTEX_POINT ( 'NONE', #115118 ) ;
#64091=ORIENTED_EDGE ( 'NONE', *, *, #14885, .T. ) ;
#64093=EDGE_LOOP ( 'NONE', ( #26042, #132738, #3220 ) ) ;
#64095=FACE_OUTER_BOUND ( 'NONE', #131322, .T. ) ;
#64096=VECTOR ( 'NONE', #74192, 999.9999999999998863 ) ;
#64097=CARTESIAN_POINT ( 'NONE',  ( -6.489213562373093325, -27.52281430457059841, 5.000000000000000000 ) ) ;
#64099=FACE_BOUND ( 'NONE', #52129, .T. ) ;
#64100=CARTESIAN_POINT ( 'NONE',  ( 45.48921356237309510, -27.52281430457087197, 5.000000000000000000 ) ) ;
#64104=DIRECTION ( 'NONE',  ( -0.000000000000000000, -0.3543493200069152693, 0.9351131265310292928 ) ) ;
#64105=VERTEX_POINT ( 'NONE', #61533 ) ;
#64106=DIRECTION ( 'NONE',  ( 0.3543493200069162685, -0.000000000000000000, -0.9351131265310288487 ) ) ;
#64108=VECTOR ( 'NONE', #105301, 1000.000000000000114 ) ;
#64110=EDGE_CURVE ( 'NONE', #13100, #29497, #15789, .T. ) ;
#64111=EDGE_CURVE ( 'NONE', #42005, #14007, #81126, .T. ) ;
#64112=ORIENTED_EDGE ( 'NONE', *, *, #101411, .F. ) ;
#64114=ORIENTED_EDGE ( 'NONE', *, *, #138997, .T. ) ;
#64115=CARTESIAN_POINT ( 'NONE',  ( -8.510786437626906675, -27.52281430457049183, 5.000000000000000000 ) ) ;
#64116=ADVANCED_FACE ( 'NONE', ( #60084 ), #50619, .T. ) ;
#64117=AXIS2_PLACEMENT_3D ( 'NONE', #44528, #24163, #66963 ) ;
#64118=CARTESIAN_POINT ( 'NONE',  ( -28.49999999999979750, 3.431123077392151277, 4.000000000000000000 ) ) ;
#64120=ORIENTED_EDGE ( 'NONE', *, *, #21636, .F. ) ;
#64121=FACE_OUTER_BOUND ( 'NONE', #2384, .T. ) ;
#64124=PLANE ( 'NONE',  #48387 ) ;
#64125=EDGE_CURVE ( 'NONE', #70281, #94584, #105680, .T. ) ;
#64126=LINE ( 'NONE', #10432, #87180 ) ;
#64127=DIRECTION ( 'NONE',  ( 0.7071067811865486830, -0.7071067811865464625, -0.000000000000000000 ) ) ;
#64128=FACE_OUTER_BOUND ( 'NONE', #8781, .T. ) ;
#64129=DIRECTION ( 'NONE',  ( -0.7071067811865486830, -0.7071067811865464625, 0.000000000000000000 ) ) ;
#64130=CARTESIAN_POINT ( 'NONE',  ( 13.49999999999990763, -11.94781430457070748, 5.000000000000000000 ) ) ;
#64131=ORIENTED_EDGE ( 'NONE', *, *, #41550, .F. ) ;
#64133=ORIENTED_EDGE ( 'NONE', *, *, #88385, .T. ) ;
#64134=CARTESIAN_POINT ( 'NONE',  ( 21.32816939922336985, -6.740707523384216415, 4.000000000000000000 ) ) ;
#64135=DIRECTION ( 'NONE',  ( -0.6830127018922181881, 0.6830127018922202975, -0.2588190451025214056 ) ) ;
#64136=EDGE_CURVE ( 'NONE', #37795, #141564, #4919, .T. ) ;
#64137=EDGE_LOOP ( 'NONE', ( #33872, #127779, #54126, #139516 ) ) ;
#64138=AXIS2_PLACEMENT_3D ( 'NONE', #100291, #122007, #66943 ) ;
#64139=ORIENTED_EDGE ( 'NONE', *, *, #94042, .T. ) ;
#64140=PLANE ( 'NONE',  #126243 ) ;
#64141=ORIENTED_EDGE ( 'NONE', *, *, #75018, .F. ) ;
#64143=ORIENTED_EDGE ( 'NONE', *, *, #106454, .F. ) ;
#64145=EDGE_CURVE ( 'NONE', #37768, #8478, #115833, .T. ) ;
#64146=VECTOR ( 'NONE', #12553, 1000.000000000000227 ) ;
#64147=VECTOR ( 'NONE', #63055, 1000.000000000000000 ) ;
#64148=VECTOR ( 'NONE', #134305, 1000.000000000000227 ) ;
#64152=EDGE_LOOP ( 'NONE', ( #50970, #74703, #18362, #16109 ) ) ;
#64155=ORIENTED_EDGE ( 'NONE', *, *, #91294, .T. ) ;
#64156=LINE ( 'NONE', #122804, #136746 ) ;
#64157=VECTOR ( 'NONE', #117000, 1000.000000000000000 ) ;
#64158=PLANE ( 'NONE',  #75339 ) ;
#64159=LINE ( 'NONE', #32983, #3070 ) ;
#64160=EDGE_LOOP ( 'NONE', ( #63056, #21230, #27147, #103465 ) ) ;
#64161=EDGE_LOOP ( 'NONE', ( #4063, #112246, #12337, #114326 ) ) ;
#64162=CARTESIAN_POINT ( 'NONE',  ( 12.32816939922343913, -9.740707523384184441, 4.000000000000000000 ) ) ;
#64163=CARTESIAN_POINT ( 'NONE',  ( 33.79333936457825160, 21.75929247661550647, 4.998822639870711626 ) ) ;
#64164=ORIENTED_EDGE ( 'NONE', *, *, #132612, .F. ) ;
#64166=VERTEX_POINT ( 'NONE', #127457 ) ;
#64167=ORIENTED_EDGE ( 'NONE', *, *, #136235, .F. ) ;
#64168=ORIENTED_EDGE ( 'NONE', *, *, #69363, .T. ) ;
#64169=ADVANCED_FACE ( 'NONE', ( #28157 ), #39769, .F. ) ;
#64170=CARTESIAN_POINT ( 'NONE',  ( 1.499999999999987566, -17.91344420646042579, 1.358650452708467737 ) ) ;
#64171=CARTESIAN_POINT ( 'NONE',  ( -36.48921356237310221, -27.52281430457080802, 5.000000000000000000 ) ) ;
#64173=ADVANCED_FACE ( 'NONE', ( #108521 ), #86107, .F. ) ;
#64175=DIRECTION ( 'NONE',  ( 0.7071067811865487940, 0.7071067811865463515, -0.000000000000000000 ) ) ;
#64179=ORIENTED_EDGE ( 'NONE', *, *, #343, .F. ) ;
#64180=AXIS2_PLACEMENT_3D ( 'NONE', #134591, #81643, #125108 ) ;
#64181=CARTESIAN_POINT ( 'NONE',  ( -34.47516574401890921, -19.50948238788419076, 4.998110765256836174 ) ) ;
#64182=( BOUNDED_CURVE ( )  B_SPLINE_CURVE ( 3, ( #91544, #124876, #12531, #35039 ),
 .UNSPECIFIED., .F., .T. ) 
 B_SPLINE_CURVE_WITH_KNOTS ( ( 4, 4 ),
 ( 5.106027341939272546, 6.645403452391245303 ),
 .UNSPECIFIED. ) 
 CURVE ( )  GEOMETRIC_REPRESENTATION_ITEM ( )  RATIONAL_B_SPLINE_CURVE ( ( 1.000000000000000000, 0.8120851936182260644, 0.8120851936182260644, 1.000000000000000000 ) ) 
 REPRESENTATION_ITEM ( '' )  );
#64183=ADVANCED_FACE ( 'NONE', ( #117969 ), #128880, .T. ) ;
#64185=VERTEX_POINT ( 'NONE', #75252 ) ;
#64187=CARTESIAN_POINT ( 'NONE',  ( 10.82816939922345512, -2.240707523384264377, 4.000000000000000000 ) ) ;
#64188=VERTEX_POINT ( 'NONE', #62949 ) ;
#64189=ORIENTED_EDGE ( 'NONE', *, *, #85641, .F. ) ;
#64191=CARTESIAN_POINT ( 'NONE',  ( -13.75179860200718984, 5.925774409307371648, 4.669108085256721274 ) ) ;
#64192=CARTESIAN_POINT ( 'NONE',  ( 0.000000000000000000, 0.000000000000000000, 5.000000000000000000 ) ) ;
#64195=CARTESIAN_POINT ( 'NONE',  ( 22.96641869250914070, 7.680402717527123890, 4.333886692633072357 ) ) ;
#64197=CARTESIAN_POINT ( 'NONE',  ( -24.79289321881327623, 18.75929247661552068, 5.000000000000000000 ) ) ;
#64198=DIRECTION ( 'NONE',  ( 0.7071067811865486830, -0.7071067811865464625, -0.000000000000000000 ) ) ;
#64201=EDGE_LOOP ( 'NONE', ( #23484, #114058, #98503, #13066 ) ) ;
#64202=CARTESIAN_POINT ( 'NONE',  ( 0.000000000000000000, 0.000000000000000000, 5.000000000000000000 ) ) ;
#64205=DIRECTION ( 'NONE',  ( 0.7071067811865487940, -0.7071067811865463515, 0.000000000000000000 ) ) ;
#64206=LINE ( 'NONE', #85216, #19851 ) ;
#64208=LINE ( 'NONE', #9046, #83196 ) ;
#64209=CARTESIAN_POINT ( 'NONE',  ( 16.49999999999989342, 13.46639925780212010, 5.000000000000000000 ) ) ;
#64210=ORIENTED_EDGE ( 'NONE', *, *, #82180, .T. ) ;
#64212=AXIS2_PLACEMENT_3D ( 'NONE', #33985, #102814, #69482 ) ;
#64213=EDGE_CURVE ( 'NONE', #13173, #53146, #140469, .T. ) ;
#64214=CARTESIAN_POINT ( 'NONE',  ( 34.92499999999998295, -21.28150956279551664, 4.759050581649326261 ) ) ;
#64215=LINE ( 'NONE', #87396, #12510 ) ;
#64217=ORIENTED_EDGE ( 'NONE', *, *, #1571, .F. ) ;
#64218=DIRECTION ( 'NONE',  ( -0.6830127018922180770, -0.6830127018922204085, -0.2588190451025213501 ) ) ;
#64219=PLANE ( 'NONE',  #23644 ) ;
#64220=DIRECTION ( 'NONE',  ( -0.000000000000000000, -0.3543493200069152693, 0.9351131265310292928 ) ) ;
#64222=DIRECTION ( 'NONE',  ( 0.7071067811865486830, -0.7071067811865464625, -0.000000000000000000 ) ) ;
#64223=CARTESIAN_POINT ( 'NONE',  ( 15.08314806772921557, 21.75929247661549937, 7.311836541448085036 ) ) ;
#64224=ORIENTED_EDGE ( 'NONE', *, *, #19102, .F. ) ;
#64226=CARTESIAN_POINT ( 'NONE',  ( -34.92500000000001137, 22.22500000000000142, 4.500000000000000888 ) ) ;
#64228=ORIENTED_EDGE ( 'NONE', *, *, #39936, .F. ) ;
#64231=VECTOR ( 'NONE', #109852, 1000.000000000000000 ) ;
#64232=EDGE_CURVE ( 'NONE', #119557, #96580, #7064, .T. ) ;
#64234=DIRECTION ( 'NONE',  ( -0.6830127018922180770, -0.6830127018922204085, -0.2588190451025214056 ) ) ;
#64236=ORIENTED_EDGE ( 'NONE', *, *, #15073, .T. ) ;
#64237=DIRECTION ( 'NONE',  ( 0.7071067811865487940, -0.7071067811865463515, 0.000000000000000000 ) ) ;
#64238=CARTESIAN_POINT ( 'NONE',  ( -26.99451991528749417, 28.92564299267956685, 4.000000000000000000 ) ) ;
#64239=VECTOR ( 'NONE', #70729, 1000.000000000000000 ) ;
#64240=CARTESIAN_POINT ( 'NONE',  ( -30.32816939922331301, 8.259292476615636147, 4.000000000000000000 ) ) ;
#64242=LINE ( 'NONE', #98302, #62513 ) ;
#64243=CARTESIAN_POINT ( 'NONE',  ( 34.47516574401891631, -2.971932658884160361, 4.998110765256834398 ) ) ;
#64244=ORIENTED_EDGE ( 'NONE', *, *, #24543, .F. ) ;
#64245=PLANE ( 'NONE',  #138678 ) ;
#64247=CARTESIAN_POINT ( 'NONE',  ( 23.42830866441052962, 7.233000843196646379, 4.333645886165172101 ) ) ;
#64249=CARTESIAN_POINT ( 'NONE',  ( 2.999999999999995559, -16.44781430457066662, 5.000000000000000000 ) ) ;
#64250=VECTOR ( 'NONE', #76422, 1000.000000000000227 ) ;
#64251=ORIENTED_EDGE ( 'NONE', *, *, #50171, .F. ) ;
#64252=EDGE_LOOP ( 'NONE', ( #69665, #2963, #112195, #127056 ) ) ;
#64253=VECTOR ( 'NONE', #23958, 999.9999999999998863 ) ;
#64255=ORIENTED_EDGE ( 'NONE', *, *, #5017, .F. ) ;
#64256=DIRECTION ( 'NONE',  ( 0.7071067811865487940, 0.7071067811865463515, 0.000000000000000000 ) ) ;
#64259=AXIS2_PLACEMENT_3D ( 'NONE', #56458, #100633, #78170 ) ;
#64261=ORIENTED_EDGE ( 'NONE', *, *, #40253, .F. ) ;
#64262=DIRECTION ( 'NONE',  ( -0.7071067811865487940, 0.7071067811865463515, -0.000000000000000000 ) ) ;
#64263=LINE ( 'NONE', #30933, #14334 ) ;
#64264=EDGE_LOOP ( 'NONE', ( #59016, #106978, #47874, #9977 ) ) ;
#64265=CARTESIAN_POINT ( 'NONE',  ( 24.18398860626899705, 28.73617430169804265, 5.000000000000000000 ) ) ;
#64266=EDGE_CURVE ( 'NONE', #18293, #44324, #96932, .T. ) ;
#64267=CARTESIAN_POINT ( 'NONE',  ( 13.49999999999991473, 13.46639925780212366, 5.000000000000000000 ) ) ;
#64268=CARTESIAN_POINT ( 'NONE',  ( -13.11547925347946908, 3.815643823912585386, 4.000000000000000000 ) ) ;
#64269=ORIENTED_EDGE ( 'NONE', *, *, #34872, .F. ) ;
#64270=ORIENTED_EDGE ( 'NONE', *, *, #55411, .F. ) ;
#64271=FACE_BOUND ( 'NONE', #102829, .T. ) ;
#64272=LINE ( 'NONE', #9118, #119539 ) ;
#64274=FACE_OUTER_BOUND ( 'NONE', #39187, .T. ) ;
#64275=VECTOR ( 'NONE', #1694, 1000.000000000000000 ) ;
#64276=PLANE ( 'NONE',  #11001 ) ;
#64277=PLANE ( 'NONE',  #69795 ) ;
#64278=VERTEX_POINT ( 'NONE', #19410 ) ;
#64279=EDGE_CURVE ( 'NONE', #96885, #114780, #130335, .T. ) ;
#64280=AXIS2_PLACEMENT_3D ( 'NONE', #62229, #41896, #106383 ) ;
#64281=ORIENTED_EDGE ( 'NONE', *, *, #89951, .F. ) ;
#64284=EDGE_CURVE ( 'NONE', #29435, #96265, #63664, .T. ) ;
#64285=ADVANCED_FACE ( 'NONE', ( #9198 ), #73110, .F. ) ;
#64286=EDGE_LOOP ( 'NONE', ( #59571, #33268, #23955, #102381 ) ) ;
#64287=EDGE_CURVE ( 'NONE', #26316, #113825, #83995, .T. ) ;
#64288=CARTESIAN_POINT ( 'NONE',  ( -15.98911971346040062, -22.02621442084248571, 4.990779571109219326 ) ) ;
#64290=CARTESIAN_POINT ( 'NONE',  ( 15.52400138585438683, 22.03583458319438648, 4.979811245910089390 ) ) ;
#64291=CARTESIAN_POINT ( 'NONE',  ( 0.000000000000000000, 0.000000000000000000, 5.000000000000000000 ) ) ;
#64293=CARTESIAN_POINT ( 'NONE',  ( -28.49999999999981171, 22.22500000000000853, 4.362957392718823435 ) ) ;
#64294=CARTESIAN_POINT ( 'NONE',  ( -2.999999999999978240, 20.96639925780204550, 5.000000000000000000 ) ) ;
#64295=ADVANCED_FACE ( 'NONE', ( #54917 ), #67964, .F. ) ;
#64297=DIRECTION ( 'NONE',  ( -0.6830127018922181881, 0.6830127018922202975, -0.2588190451025214056 ) ) ;
#64298=DIRECTION ( 'NONE',  ( 0.7071067811865486830, -0.7071067811865464625, -0.000000000000000000 ) ) ;
#64300=CARTESIAN_POINT ( 'NONE',  ( 4.171830600776446296, 21.75929247661550292, 4.000000000000000000 ) ) ;
#64301=CARTESIAN_POINT ( 'NONE',  ( -5.999999999999967137, 4.931123077392134846, 4.000000000000000000 ) ) ;
#64302=ADVANCED_FACE ( 'NONE', ( #88978 ), #55626, .F. ) ;
#64303=AXIS2_PLACEMENT_3D ( 'NONE', #107771, #108459, #88929 ) ;
#64304=ORIENTED_EDGE ( 'NONE', *, *, #95469, .T. ) ;
#64305=LINE ( 'NONE', #97629, #27367 ) ;
#64311=ORIENTED_EDGE ( 'NONE', *, *, #135802, .T. ) ;
#64313=ADVANCED_FACE ( 'NONE', ( #111405 ), #78805, .F. ) ;
#64314=LINE ( 'NONE', #54186, #115957 ) ;
#64315=AXIS2_PLACEMENT_3D ( 'NONE', #26499, #37379, #17728 ) ;
#64317=DIRECTION ( 'NONE',  ( -0.3543493200069162685, -0.000000000000000000, -0.9351131265310288487 ) ) ;
#64320=DIRECTION ( 'NONE',  ( -0.000000000000000000, 0.3543493200069153248, 0.9351131265310292928 ) ) ;
#64321=ADVANCED_FACE ( 'NONE', ( #112839 ), #88253, .F. ) ;
#64322=CARTESIAN_POINT ( 'NONE',  ( -4.171830600776443632, 6.759292476615649470, 4.000000000000000000 ) ) ;
#64326=AXIS2_PLACEMENT_3D ( 'NONE', #69790, #68365, #91515 ) ;
#64329=VERTEX_POINT ( 'NONE', #1204 ) ;
#64330=EDGE_LOOP ( 'NONE', ( #105370, #107759, #125618, #75881 ) ) ;
#64331=ADVANCED_FACE ( 'NONE', ( #22239, #133891, #11350 ), #56375, .F. ) ;
#64334=VECTOR ( 'NONE', #49013, 1000.000000000000000 ) ;
#64335=DIRECTION ( 'NONE',  ( -0.7071067811865487940, 0.7071067811865463515, -0.000000000000000000 ) ) ;
#64336=PLANE ( 'NONE',  #108118 ) ;
#64338=CARTESIAN_POINT ( 'NONE',  ( 25.17183060077629619, -8.240707523384198652, 4.000000000000000000 ) ) ;
#64339=ORIENTED_EDGE ( 'NONE', *, *, #94822, .T. ) ;
#64340=ORIENTED_EDGE ( 'NONE', *, *, #3303, .T. ) ;
#64341=VECTOR ( 'NONE', #80729, 1000.000000000000000 ) ;
#64343=EDGE_CURVE ( 'NONE', #98816, #50789, #78094, .T. ) ;
#64345=FACE_OUTER_BOUND ( 'NONE', #130695, .T. ) ;
#64347=ORIENTED_EDGE ( 'NONE', *, *, #132035, .T. ) ;
#64348=VERTEX_POINT ( 'NONE', #23697 ) ;
#64349=EDGE_CURVE ( 'NONE', #143112, #13174, #66505, .T. ) ;
#64350=VERTEX_POINT ( 'NONE', #12802 ) ;
#64353=CARTESIAN_POINT ( 'NONE',  ( 26.99451991528749417, 28.92564299267956685, 4.000000000000000000 ) ) ;
#64354=FACE_OUTER_BOUND ( 'NONE', #17655, .T. ) ;
#64355=DIRECTION ( 'NONE',  ( 1.000000000000000000, 0.000000000000000000, 0.000000000000000000 ) ) ;
#64356=DIRECTION ( 'NONE',  ( -0.7071067811865486830, -0.7071067811865464625, 0.000000000000000000 ) ) ;
#64358=EDGE_CURVE ( 'NONE', #332, #101734, #99086, .T. ) ;
#64359=DIRECTION ( 'NONE',  ( 0.3543493200069163240, -0.000000000000000000, -0.9351131265310288487 ) ) ;
#64360=CARTESIAN_POINT ( 'NONE',  ( 14.70025512860841133, -27.71228299555195917, 4.000000000000000000 ) ) ;
#64361=VERTEX_POINT ( 'NONE', #134626 ) ;
#64362=PLANE ( 'NONE',  #92784 ) ;
#64365=VERTEX_POINT ( 'NONE', #33189 ) ;
#64366=VECTOR ( 'NONE', #100178, 1000.000000000000000 ) ;
#64367=DIRECTION ( 'NONE',  ( -0.7071067811865486830, -0.7071067811865464625, 0.000000000000000000 ) ) ;
#64368=PLANE ( 'NONE',  #51091 ) ;
#64369=EDGE_LOOP ( 'NONE', ( #8527, #37867, #109069, #142712 ) ) ;
#64370=ADVANCED_FACE ( 'NONE', ( #77403 ), #48303, .F. ) ;
#64374=ORIENTED_EDGE ( 'NONE', *, *, #10890, .F. ) ;
#64375=CARTESIAN_POINT ( 'NONE',  ( -53.99451991528749062, 28.92564299267975869, 4.000000000000000000 ) ) ;
#64377=CARTESIAN_POINT ( 'NONE',  ( -15.48921356237309510, -27.52281430457066236, 5.000000000000000000 ) ) ;
#64379=FACE_OUTER_BOUND ( 'NONE', #71055, .T. ) ;
#64380=DIRECTION ( 'NONE',  ( -0.7071067811865487940, 0.7071067811865463515, 0.000000000000000000 ) ) ;
#64381=FACE_OUTER_BOUND ( 'NONE', #140195, .T. ) ;
#64383=PLANE ( 'NONE',  #39232 ) ;
#64386=DIRECTION ( 'NONE',  ( -0.7071067811865486830, -0.7071067811865464625, 0.000000000000000000 ) ) ;
#64387=FACE_OUTER_BOUND ( 'NONE', #41156, .T. ) ;
#64388=ORIENTED_EDGE ( 'NONE', *, *, #117008, .F. ) ;
#64390=ORIENTED_EDGE ( 'NONE', *, *, #120189, .T. ) ;
#64391=LINE ( 'NONE', #45529, #58268 ) ;
#64392=ORIENTED_EDGE ( 'NONE', *, *, #4938, .T. ) ;
#64395=CARTESIAN_POINT ( 'NONE',  ( 29.99999999999978328, -13.39766691384881092, -10.96608748226472763 ) ) ;
#64397=VERTEX_POINT ( 'NONE', #2639 ) ;
#64399=DIRECTION ( 'NONE',  ( 0.6830127018922181881, 0.6830127018922202975, -0.2588190451025214056 ) ) ;
#64401=ADVANCED_FACE ( 'NONE', ( #47636 ), #127283, .F. ) ;
#64402=ADVANCED_FACE ( 'NONE', ( #15624 ), #135343, .T. ) ;
#64404=PLANE ( 'NONE',  #139993 ) ;
#64405=VERTEX_POINT ( 'NONE', #49768 ) ;
#64408=DIRECTION ( 'NONE',  ( -0.7071067811865486830, 0.7071067811865464625, 0.000000000000000000 ) ) ;
#64409=FACE_OUTER_BOUND ( 'NONE', #94697, .T. ) ;
#64410=ORIENTED_EDGE ( 'NONE', *, *, #124420, .F. ) ;
#64411=ORIENTED_EDGE ( 'NONE', *, *, #118284, .T. ) ;
#64412=EDGE_LOOP ( 'NONE', ( #21707, #2259, #109548, #120066 ) ) ;
#64415=EDGE_LOOP ( 'NONE', ( #70861, #101947, #41836, #134019 ) ) ;
#64417=PLANE ( 'NONE',  #75849 ) ;
#64418=VERTEX_POINT ( 'NONE', #27983 ) ;
#64419=ADVANCED_FACE ( 'NONE', ( #46937 ), #80250, .F. ) ;
#64421=DIRECTION ( 'NONE',  ( -0.7071067811865486830, -0.7071067811865464625, 0.000000000000000000 ) ) ;
#64423=ORIENTED_EDGE ( 'NONE', *, *, #127480, .F. ) ;
#64424=VECTOR ( 'NONE', #115289, 1000.000000000000000 ) ;
#64426=LINE ( 'NONE', #30370, #73133 ) ;
#64427=LINE ( 'NONE', #55003, #100199 ) ;
#64428=VECTOR ( 'NONE', #4176, 1000.000000000000000 ) ;
#64429=CARTESIAN_POINT ( 'NONE',  ( 0.000000000000000000, 0.000000000000000000, 5.000000000000000000 ) ) ;
#64430=ORIENTED_EDGE ( 'NONE', *, *, #129141, .F. ) ;
#64431=ORIENTED_EDGE ( 'NONE', *, *, #134066, .F. ) ;
#64432=VECTOR ( 'NONE', #14876, 999.9999999999998863 ) ;
#64437=VECTOR ( 'NONE', #143464, 1000.000000000000114 ) ;
#64438=VECTOR ( 'NONE', #125281, 1000.000000000000000 ) ;
#64439=DIRECTION ( 'NONE',  ( -0.3543493200069162685, -0.000000000000000000, -0.9351131265310288487 ) ) ;
#64440=CARTESIAN_POINT ( 'NONE',  ( -11.18753812416045257, -22.22500000000000142, 4.000000000000000000 ) ) ;
#64443=ORIENTED_EDGE ( 'NONE', *, *, #13608, .T. ) ;
#64444=ORIENTED_EDGE ( 'NONE', *, *, #88518, .T. ) ;
#64445=EDGE_CURVE ( 'NONE', #121029, #22536, #82380, .T. ) ;
#64446=CARTESIAN_POINT ( 'NONE',  ( -17.29298673570684386, -21.74070752338406720, 4.999753212805220670 ) ) ;
#64448=ORIENTED_EDGE ( 'NONE', *, *, #50327, .T. ) ;
#64449=EDGE_CURVE ( 'NONE', #52608, #15705, #4023, .T. ) ;
#64450=EDGE_CURVE ( 'NONE', #67554, #122496, #115660, .T. ) ;
#64451=VECTOR ( 'NONE', #25869, 1000.000000000000000 ) ;
#64453=CARTESIAN_POINT ( 'NONE',  ( 36.29974487139159578, -27.71228299555231445, 4.000000000000000000 ) ) ;
#64454=ORIENTED_EDGE ( 'NONE', *, *, #14510, .T. ) ;
#64456=DIRECTION ( 'NONE',  ( -0.7071067811865486830, -0.7071067811865464625, 0.000000000000000000 ) ) ;
#64457=DIRECTION ( 'NONE',  ( -0.6830127018922181881, 0.6830127018922202975, -0.2588190451025214056 ) ) ;
#64458=DIRECTION ( 'NONE',  ( -0.7071067811865487940, 0.7071067811865463515, 0.000000000000000000 ) ) ;
#64459=VECTOR ( 'NONE', #47844, 1000.000000000000000 ) ;
#64460=DIRECTION ( 'NONE',  ( -0.000000000000000000, 0.000000000000000000, 1.000000000000000000 ) ) ;
#64461=ORIENTED_EDGE ( 'NONE', *, *, #69177, .T. ) ;
#64463=CARTESIAN_POINT ( 'NONE',  ( 71.99451991528749772, 28.92564299267988304, 4.000000000000000000 ) ) ;
#64465=EDGE_CURVE ( 'NONE', #17205, #130681, #58529, .T. ) ;
#64466=ORIENTED_EDGE ( 'NONE', *, *, #18622, .T. ) ;
#64467=DIRECTION ( 'NONE',  ( 0.6830127018922181881, 0.6830127018922202975, -0.2588190451025214056 ) ) ;
#64470=CARTESIAN_POINT ( 'NONE',  ( -20.99451991528748707, 28.92564299267952777, 4.000000000000000000 ) ) ;
#64471=EDGE_CURVE ( 'NONE', #80773, #43157, #116423, .T. ) ;
#64472=ORIENTED_EDGE ( 'NONE', *, *, #112885, .F. ) ;
#64473=LINE ( 'NONE', #5777, #38985 ) ;
#64474=EDGE_LOOP ( 'NONE', ( #83928, #73604, #26716, #53185 ) ) ;
#64475=VERTEX_POINT ( 'NONE', #103373 ) ;
#64476=ORIENTED_EDGE ( 'NONE', *, *, #95541, .F. ) ;
#64477=EDGE_CURVE ( 'NONE', #28064, #74252, #38862, .T. ) ;
#64479=DIRECTION ( 'NONE',  ( -0.000000000000000000, 0.000000000000000000, 1.000000000000000000 ) ) ;
#64480=FACE_OUTER_BOUND ( 'NONE', #28832, .T. ) ;
#64482=FACE_OUTER_BOUND ( 'NONE', #5741, .T. ) ;
#64483=FACE_OUTER_BOUND ( 'NONE', #22032, .T. ) ;
#64484=EDGE_CURVE ( 'NONE', #129447, #5674, #71496, .T. ) ;
#64486=LINE ( 'NONE', #11491, #28448 ) ;
#64487=AXIS2_PLACEMENT_3D ( 'NONE', #138733, #39426, #83659 ) ;
#64488=CARTESIAN_POINT ( 'NONE',  ( -3.299744871391591339, -27.71228299555208352, 4.000000000000000000 ) ) ;
#64489=CARTESIAN_POINT ( 'NONE',  ( 23.99999999999981881, -16.02097659208070368, -11.96015758381214766 ) ) ;
#64490=DIRECTION ( 'NONE',  ( 0.7071067811865487940, 0.7071067811865463515, 0.000000000000000000 ) ) ;
#64492=VERTEX_POINT ( 'NONE', #125884 ) ;
#64494=EDGE_LOOP ( 'NONE', ( #64374, #32965, #107410, #80354 ) ) ;
#64495=EDGE_LOOP ( 'NONE', ( #78598, #96335, #55391 ) ) ;
#64496=CARTESIAN_POINT ( 'NONE',  ( 0.4892135623730947680, -27.52281430457055578, 5.000000000000000000 ) ) ;
#64497=ORIENTED_EDGE ( 'NONE', *, *, #14074, .T. ) ;
#64498=ORIENTED_EDGE ( 'NONE', *, *, #98642, .F. ) ;
#64501=CARTESIAN_POINT ( 'NONE',  ( -5.207106781186503497, 0.7592924766157104211, 5.000000000000000000 ) ) ;
#64502=EDGE_CURVE ( 'NONE', #123534, #96735, #130891, .T. ) ;
#64503=EDGE_LOOP ( 'NONE', ( #7747, #63755, #12925, #114641 ) ) ;
#64504=ADVANCED_FACE ( 'NONE', ( #39595 ), #140314, .F. ) ;
#64505=DIRECTION ( 'NONE',  ( -0.3543493200069162685, -0.000000000000000000, -0.9351131265310288487 ) ) ;
#64506=ORIENTED_EDGE ( 'NONE', *, *, #142315, .T. ) ;
#64508=EDGE_CURVE ( 'NONE', #56146, #134058, #22633, .T. ) ;
#64509=CARTESIAN_POINT ( 'NONE',  ( 69.18398860626899705, 28.73617430169835529, 5.000000000000000000 ) ) ;
#64513=CARTESIAN_POINT ( 'NONE',  ( -25.82816939922334143, 3.759292476615685441, 4.000000000000000000 ) ) ;
#64514=CARTESIAN_POINT ( 'NONE',  ( 0.000000000000000000, 0.000000000000000000, 5.000000000000000000 ) ) ;
#64515=DIRECTION ( 'NONE',  ( 0.7071067811865486830, -0.7071067811865464625, -0.000000000000000000 ) ) ;
#64516=ORIENTED_EDGE ( 'NONE', *, *, #106579, .T. ) ;
#64518=CARTESIAN_POINT ( 'NONE',  ( 3.005480084712505828, 28.92564299267936079, 4.000000000000000000 ) ) ;
#64521=LINE ( 'NONE', #19583, #108978 ) ;
#64522=PLANE ( 'NONE',  #70610 ) ;
#64523=LINE ( 'NONE', #96404, #56524 ) ;
#64524=ORIENTED_EDGE ( 'NONE', *, *, #1175, .F. ) ;
#64525=DIRECTION ( 'NONE',  ( -0.000000000000000000, 0.000000000000000000, 1.000000000000000000 ) ) ;
#64526=DIRECTION ( 'NONE',  ( -0.7071067811865486830, -0.7071067811865464625, 0.000000000000000000 ) ) ;
#64527=PLANE ( 'NONE',  #129885 ) ;
#64528=ORIENTED_EDGE ( 'NONE', *, *, #65492, .T. ) ;
#64529=CARTESIAN_POINT ( 'NONE',  ( -30.48921356237309510, -27.52281430457076894, 5.000000000000000000 ) ) ;
#64531=VECTOR ( 'NONE', #1883, 1000.000000000000227 ) ;
#64532=AXIS2_PLACEMENT_3D ( 'NONE', #45068, #26126, #89241 ) ;
#64533=DIRECTION ( 'NONE',  ( -1.000000000000000000, 0.000000000000000000, 0.000000000000000000 ) ) ;
#64534=VERTEX_POINT ( 'NONE', #30862 ) ;
#64535=VECTOR ( 'NONE', #5766, 1000.000000000000227 ) ;
#64537=ORIENTED_EDGE ( 'NONE', *, *, #133337, .T. ) ;
#64538=ORIENTED_EDGE ( 'NONE', *, *, #26619, .T. ) ;
#64539=CARTESIAN_POINT ( 'NONE',  ( -84.18398860626899705, 28.73617430169846187, 5.000000000000000000 ) ) ;
#64540=DIRECTION ( 'NONE',  ( -0.000000000000000000, 0.000000000000000000, 1.000000000000000000 ) ) ;
#64541=VECTOR ( 'NONE', #117240, 999.9999999999998863 ) ;
#64542=ORIENTED_EDGE ( 'NONE', *, *, #4380, .T. ) ;
#64543=PLANE ( 'NONE',  #74377 ) ;
#64544=AXIS2_PLACEMENT_3D ( 'NONE', #105355, #128554, #107503 ) ;
#64545=CARTESIAN_POINT ( 'NONE',  ( 0.000000000000000000, 0.000000000000000000, 5.000000000000000000 ) ) ;
#64546=CARTESIAN_POINT ( 'NONE',  ( -25.49999999999982592, -17.56887692260762535, 4.000000000000000000 ) ) ;
#64547=( BOUNDED_CURVE ( )  B_SPLINE_CURVE ( 3, ( #121311, #21993, #108256, #97393 ),
 .UNSPECIFIED., .F., .T. ) 
 B_SPLINE_CURVE_WITH_KNOTS ( ( 4, 4 ),
 ( 5.143245962375970315, 6.645403452391246191 ),
 .UNSPECIFIED. ) 
 CURVE ( )  GEOMETRIC_REPRESENTATION_ITEM ( )  RATIONAL_B_SPLINE_CURVE ( ( 1.000000000000000000, 0.8206354192515253887, 0.8206354192515253887, 1.000000000000000000 ) ) 
 REPRESENTATION_ITEM ( '' )  );
#64548=LINE ( 'NONE', #53694, #32295 ) ;
#64551=LINE ( 'NONE', #119612, #137396 ) ;
#64554=LINE ( 'NONE', #10164, #86130 ) ;
#64555=VECTOR ( 'NONE', #63149, 1000.000000000000000 ) ;
#64556=CARTESIAN_POINT ( 'NONE',  ( -29.99451991528749417, 28.92564299267958816, 4.000000000000000000 ) ) ;
#64557=LINE ( 'NONE', #50833, #85872 ) ;
#64558=DIRECTION ( 'NONE',  ( -0.000000000000000000, -0.3543493200069153248, -0.9351131265310291818 ) ) ;
#64560=VERTEX_POINT ( 'NONE', #106958 ) ;
#64561=EDGE_LOOP ( 'NONE', ( #93207, #27496, #50695, #105748 ) ) ;
#64566=VERTEX_POINT ( 'NONE', #108350 ) ;
#64567=FACE_OUTER_BOUND ( 'NONE', #52257, .T. ) ;
#64568=VECTOR ( 'NONE', #131242, 1000.000000000000000 ) ;
#64569=ORIENTED_EDGE ( 'NONE', *, *, #46463, .F. ) ;
#64570=VECTOR ( 'NONE', #127170, 1000.000000000000000 ) ;
#64571=CARTESIAN_POINT ( 'NONE',  ( 3.183988606268992161, 28.73617430169789699, 5.000000000000000000 ) ) ;
#64572=AXIS2_PLACEMENT_3D ( 'NONE', #115851, #105002, #48490 ) ;
#64573=CARTESIAN_POINT ( 'NONE',  ( 34.92499999999998295, -8.240707523384182664, 4.255531930566164078 ) ) ;
#64575=LINE ( 'NONE', #76913, #92662 ) ;
#64576=PLANE ( 'NONE',  #62761 ) ;
#64578=EDGE_CURVE ( 'NONE', #30943, #91794, #141010, .T. ) ;
#64579=ORIENTED_EDGE ( 'NONE', *, *, #112900, .F. ) ;
#64580=CARTESIAN_POINT ( 'NONE',  ( 54.48921356237310221, -27.52281430457093236, 5.000000000000000000 ) ) ;
#64581=ADVANCED_FACE ( 'NONE', ( #62773 ), #139639, .F. ) ;
#64582=CARTESIAN_POINT ( 'NONE',  ( -24.72281430457042717, -21.72500000000000142, 5.000000000000000000 ) ) ;
#64583=VECTOR ( 'NONE', #102194, 1000.000000000000000 ) ;
#64585=DIRECTION ( 'NONE',  ( -0.7071067811865486830, 0.7071067811865464625, 0.000000000000000000 ) ) ;
#64586=FACE_OUTER_BOUND ( 'NONE', #98682, .T. ) ;
#64589=LINE ( 'NONE', #63200, #81663 ) ;
#64590=ORIENTED_EDGE ( 'NONE', *, *, #139148, .T. ) ;
#64591=ORIENTED_EDGE ( 'NONE', *, *, #126923, .T. ) ;
#64593=ORIENTED_EDGE ( 'NONE', *, *, #13181, .F. ) ;
#64594=EDGE_CURVE ( 'NONE', #21679, #45954, #31561, .T. ) ;
#64596=LINE ( 'NONE', #108061, #101119 ) ;
#64600=EDGE_CURVE ( 'NONE', #76199, #71344, #9025, .T. ) ;
#64601=DIRECTION ( 'NONE',  ( 0.7071067811865486830, -0.7071067811865464625, -0.000000000000000000 ) ) ;
#64602=DIRECTION ( 'NONE',  ( -0.6830127018922181881, 0.6830127018922202975, -0.2588190451025214056 ) ) ;
#64604=EDGE_LOOP ( 'NONE', ( #40657, #51612, #73713, #99848, #107312 ) ) ;
#64605=ORIENTED_EDGE ( 'NONE', *, *, #59432, .T. ) ;
#64606=LINE ( 'NONE', #20358, #2131 ) ;
#64607=EDGE_CURVE ( 'NONE', #101265, #115184, #138904, .T. ) ;
#64608=CARTESIAN_POINT ( 'NONE',  ( -60.18398860626900415, 28.73617430169829490, 5.000000000000000000 ) ) ;
#64609=CARTESIAN_POINT ( 'NONE',  ( -14.54487008052910824, -0.7407075233842735917, 4.335043535661659675 ) ) ;
#64610=ORIENTED_EDGE ( 'NONE', *, *, #49779, .T. ) ;
#64613=PLANE ( 'NONE',  #47093 ) ;
#64615=DIRECTION ( 'NONE',  ( -0.6830127018922181881, 0.6830127018922202975, -0.2588190451025214056 ) ) ;
#64617=ORIENTED_EDGE ( 'NONE', *, *, #46372, .F. ) ;
#64618=ADVANCED_FACE ( 'NONE', ( #83828 ), #128036, .T. ) ;
#64619=CARTESIAN_POINT ( 'NONE',  ( -28.99806943317882002, -22.22500000000000142, 4.500000000000000888 ) ) ;
#64620=ORIENTED_EDGE ( 'NONE', *, *, #954, .T. ) ;
#64621=ORIENTED_EDGE ( 'NONE', *, *, #96748, .F. ) ;
#64623=EDGE_CURVE ( 'NONE', #130094, #84395, #42463, .T. ) ;
#64624=EDGE_CURVE ( 'NONE', #13935, #86438, #85203, .T. ) ;
#64625=VECTOR ( 'NONE', #131942, 999.9999999999998863 ) ;
#64626=DIRECTION ( 'NONE',  ( -0.000000000000000000, -0.3543493200069152693, 0.9351131265310292928 ) ) ;
#64628=EDGE_LOOP ( 'NONE', ( #66762, #49650, #134513, #116021 ) ) ;
#64629=PLANE ( 'NONE',  #6630 ) ;
#64631=LINE ( 'NONE', #41439, #76027 ) ;
#64633=VECTOR ( 'NONE', #72797, 1000.000000000000114 ) ;
#64634=VECTOR ( 'NONE', #71389, 1000.000000000000000 ) ;
#64636=CARTESIAN_POINT ( 'NONE',  ( -36.18398860626899705, 28.73617430169812437, 5.000000000000000000 ) ) ;
#64637=VECTOR ( 'NONE', #34520, 1000.000000000000000 ) ;
#64638=FACE_BOUND ( 'NONE', #126880, .T. ) ;
#64640=ORIENTED_EDGE ( 'NONE', *, *, #21262, .T. ) ;
#64641=CARTESIAN_POINT ( 'NONE',  ( 24.48921356237309510, -27.52281430457072631, 5.000000000000000000 ) ) ;
#64642=CARTESIAN_POINT ( 'NONE',  ( 51.29974487139158867, -27.71228299555242103, 4.000000000000000000 ) ) ;
#64643=CARTESIAN_POINT ( 'NONE',  ( 27.79289321881326558, 9.759292476615625489, 5.000000000000000000 ) ) ;
#64644=EDGE_CURVE ( 'NONE', #59942, #55364, #107672, .T. ) ;
#64645=ORIENTED_EDGE ( 'NONE', *, *, #27425, .T. ) ;
#64647=VERTEX_POINT ( 'NONE', #41716 ) ;
#64648=ORIENTED_EDGE ( 'NONE', *, *, #50531, .F. ) ;
#64649=AXIS2_PLACEMENT_3D ( 'NONE', #119779, #120480, #141577 ) ;
#64650=DIRECTION ( 'NONE',  ( -0.3543493200069162685, -0.000000000000000000, -0.9351131265310288487 ) ) ;
#64651=ORIENTED_EDGE ( 'NONE', *, *, #72275, .T. ) ;
#64653=ORIENTED_EDGE ( 'NONE', *, *, #28708, .F. ) ;
#64654=EDGE_CURVE ( 'NONE', #40909, #10224, #96721, .T. ) ;
#64655=DIRECTION ( 'NONE',  ( -0.3543493200069162685, -0.000000000000000000, -0.9351131265310288487 ) ) ;
#64656=EDGE_LOOP ( 'NONE', ( #119922, #129868, #29515, #138412 ) ) ;
#64658=ORIENTED_EDGE ( 'NONE', *, *, #131848, .F. ) ;
#64659=LINE ( 'NONE', #51655, #56345 ) ;
#64660=DIRECTION ( 'NONE',  ( -0.7071067811865486830, -0.7071067811865464625, 0.000000000000000000 ) ) ;
#64662=VECTOR ( 'NONE', #54034, 1000.000000000000000 ) ;
#64665=CARTESIAN_POINT ( 'NONE',  ( -16.82816939922341248, -11.24070752338416845, 4.000000000000000000 ) ) ;
#64666=CARTESIAN_POINT ( 'NONE',  ( 28.49999999999980460, -10.91253812416064406, 4.000000000000000000 ) ) ;
#64668=CARTESIAN_POINT ( 'NONE',  ( 33.70612307739173730, 22.22500000000000142, 4.000000000000000000 ) ) ;
#64669=CARTESIAN_POINT ( 'NONE',  ( 1.171830600776464504, 15.75929247661555976, 4.000000000000000000 ) ) ;
#64670=ORIENTED_EDGE ( 'NONE', *, *, #41889, .T. ) ;
#64671=ORIENTED_EDGE ( 'NONE', *, *, #17579, .F. ) ;
#64674=DIRECTION ( 'NONE',  ( 0.7071067811865486830, -0.7071067811865464625, -0.000000000000000000 ) ) ;
#64675=DIRECTION ( 'NONE',  ( 0.3543493200069162685, -0.000000000000000000, -0.9351131265310288487 ) ) ;
#64676=ORIENTED_EDGE ( 'NONE', *, *, #114485, .F. ) ;
#64677=VECTOR ( 'NONE', #83100, 1000.000000000000227 ) ;
#64679=ORIENTED_EDGE ( 'NONE', *, *, #129468, .T. ) ;
#64680=LINE ( 'NONE', #8804, #81453 ) ;
#64681=FACE_OUTER_BOUND ( 'NONE', #80047, .T. ) ;
#64682=AXIS2_PLACEMENT_3D ( 'NONE', #52994, #85622, #141457 ) ;
#64683=CARTESIAN_POINT ( 'NONE',  ( -22.82816939922336630, -5.240707523384225297, 4.000000000000000000 ) ) ;
#64684=ORIENTED_EDGE ( 'NONE', *, *, #133262, .T. ) ;
#64686=EDGE_CURVE ( 'NONE', #96071, #130556, #54059, .T. ) ;
#64687=DIRECTION ( 'NONE',  ( -0.000000000000000000, 0.3543493200069153248, 0.9351131265310292928 ) ) ;
#64688=VECTOR ( 'NONE', #142462, 999.9999999999998863 ) ;
#64689=EDGE_CURVE ( 'NONE', #130625, #114963, #100392, .T. ) ;
#64690=LINE ( 'NONE', #87, #104558 ) ;
#64693=CARTESIAN_POINT ( 'NONE',  ( 8.999999999999937828, -16.06887692260764666, 4.000000000000000000 ) ) ;
#64696=DIRECTION ( 'NONE',  ( 0.6830127018922180770, -0.6830127018922204085, -0.2588190451025213501 ) ) ;
#64697=CARTESIAN_POINT ( 'NONE',  ( 29.99999999999978684, -7.068876922607743474, 4.000000000000000000 ) ) ;
#64699=CARTESIAN_POINT ( 'NONE',  ( -33.18398860626899705, 28.73617430169810305, 5.000000000000000000 ) ) ;
#64700=ORIENTED_EDGE ( 'NONE', *, *, #140677, .T. ) ;
#64701=FACE_OUTER_BOUND ( 'NONE', #6076, .T. ) ;
#64703=CARTESIAN_POINT ( 'NONE',  ( -23.55512991947090029, -0.7407075233842665973, 4.307968247156982677 ) ) ;
#64705=LINE ( 'NONE', #43655, #98079 ) ;
#64707=CARTESIAN_POINT ( 'NONE',  ( -45.18398860626900415, 28.73617430169818832, 5.000000000000000000 ) ) ;
#64708=LINE ( 'NONE', #129226, #141698 ) ;
#64709=VERTEX_POINT ( 'NONE', #98247 ) ;
#64710=DIRECTION ( 'NONE',  ( -0.7071067811865486830, -0.7071067811865464625, 0.000000000000000000 ) ) ;
#64711=DIRECTION ( 'NONE',  ( 0.7071067811865486830, -0.7071067811865464625, -0.000000000000000000 ) ) ;
#64713=DIRECTION ( 'NONE',  ( -0.7071067811865486830, -0.7071067811865464625, -0.000000000000000000 ) ) ;
#64714=CARTESIAN_POINT ( 'NONE',  ( 5.510786437626906675, -27.52281430457051314, 5.000000000000000000 ) ) ;
#64715=EDGE_LOOP ( 'NONE', ( #123269, #113043, #35395 ) ) ;
#64716=ORIENTED_EDGE ( 'NONE', *, *, #69354, .T. ) ;
#64717=CARTESIAN_POINT ( 'NONE',  ( 2.510786437626908008, -27.52281430457053446, 5.000000000000000000 ) ) ;
#64721=LINE ( 'NONE', #75607, #137052 ) ;
#64722=ORIENTED_EDGE ( 'NONE', *, *, #117390, .F. ) ;
#64723=FACE_OUTER_BOUND ( 'NONE', #74202, .T. ) ;
#64724=CARTESIAN_POINT ( 'NONE',  ( 72.29974487139158157, -27.71228299555256669, 4.000000000000000000 ) ) ;
#64725=CARTESIAN_POINT ( 'NONE',  ( -4.499999999999966249, -1.533600742197721134, 5.000000000000000000 ) ) ;
#64726=DIRECTION ( 'NONE',  ( -0.000000000000000000, -0.3543493200069152693, 0.9351131265310292928 ) ) ;
#64729=VERTEX_POINT ( 'NONE', #10493 ) ;
#64730=ORIENTED_EDGE ( 'NONE', *, *, #20518, .T. ) ;
#64731=DIRECTION ( 'NONE',  ( -0.6830127018922180770, -0.6830127018922204085, -0.2588190451025213501 ) ) ;
#64732=EDGE_LOOP ( 'NONE', ( #110019, #50617, #104359, #90455 ) ) ;
#64733=VERTEX_POINT ( 'NONE', #11921 ) ;
#64734=VECTOR ( 'NONE', #117890, 1000.000000000000000 ) ;
#64735=CARTESIAN_POINT ( 'NONE',  ( 24.18398860626899705, 28.73617430169804265, 5.000000000000000000 ) ) ;
#64736=PLANE ( 'NONE',  #113282 ) ;
#64737=VECTOR ( 'NONE', #91596, 1000.000000000000000 ) ;
#64740=VERTEX_POINT ( 'NONE', #89498 ) ;
#64742=CARTESIAN_POINT ( 'NONE',  ( 69.48921356237309510, -27.52281430457103895, 5.000000000000000000 ) ) ;
#64744=EDGE_CURVE ( 'NONE', #58453, #100009, #9788, .T. ) ;
#64745=DIRECTION ( 'NONE',  ( -0.7071067811865486830, -0.7071067811865464625, 0.000000000000000000 ) ) ;
#64746=DIRECTION ( 'NONE',  ( -0.7071067811865486830, -0.7071067811865464625, 0.000000000000000000 ) ) ;
#64747=CARTESIAN_POINT ( 'NONE',  ( 32.99451991528749062, 28.92564299267960948, 4.000000000000000000 ) ) ;
#64748=ADVANCED_FACE ( 'NONE', ( #142471 ), #122846, .T. ) ;
#64749=EDGE_CURVE ( 'NONE', #128517, #41026, #33019, .T. ) ;
#64754=LINE ( 'NONE', #53139, #34015 ) ;
#64755=CARTESIAN_POINT ( 'NONE',  ( -9.489213562373095101, -27.52281430457062328, 5.000000000000000000 ) ) ;
#64757=LINE ( 'NONE', #98787, #57416 ) ;
#64758=EDGE_CURVE ( 'NONE', #43661, #74078, #133733, .T. ) ;
#64760=EDGE_CURVE ( 'NONE', #13171, #100977, #11180, .T. ) ;
#64761=CARTESIAN_POINT ( 'NONE',  ( -66.18398860626901126, 28.73617430169833753, 5.000000000000000000 ) ) ;
#64762=VECTOR ( 'NONE', #63998, 1000.000000000000000 ) ;
#64763=ORIENTED_EDGE ( 'NONE', *, *, #10640, .T. ) ;
#64764=ORIENTED_EDGE ( 'NONE', *, *, #102224, .T. ) ;
#64766=CARTESIAN_POINT ( 'NONE',  ( 19.49999999999986500, -10.04351517176476172, -1.623559851933778830 ) ) ;
#64767=EDGE_CURVE ( 'NONE', #112641, #77505, #55458, .T. ) ;
#64768=LINE ( 'NONE', #85790, #117929 ) ;
#64769=VECTOR ( 'NONE', #74760, 1000.000000000000227 ) ;
#64770=AXIS2_PLACEMENT_3D ( 'NONE', #134193, #46, #66787 ) ;
#64771=CARTESIAN_POINT ( 'NONE',  ( 33.70710678118631165, -15.74070752338412049, 5.000000000000000000 ) ) ;
#64772=ORIENTED_EDGE ( 'NONE', *, *, #93579, .T. ) ;
#64773=DIRECTION ( 'NONE',  ( 0.7071067811865487940, 0.7071067811865463515, 0.000000000000000000 ) ) ;
#64774=PLANE ( 'NONE',  #104663 ) ;
#64775=EDGE_CURVE ( 'NONE', #111906, #85516, #23524, .T. ) ;
#64778=EDGE_LOOP ( 'NONE', ( #110020, #140392, #55752, #120956 ) ) ;
#64779=CARTESIAN_POINT ( 'NONE',  ( -34.92500000000001137, 22.22500000000000142, 4.000000000000000000 ) ) ;
#64780=VERTEX_POINT ( 'NONE', #99646 ) ;
#64782=PLANE ( 'NONE',  #100471 ) ;
#64783=AXIS2_PLACEMENT_3D ( 'NONE', #134338, #89389, #23404 ) ;
#64784=EDGE_CURVE ( 'NONE', #142812, #59733, #317, .T. ) ;
#64786=LINE ( 'NONE', #42333, #33842 ) ;
#64787=CARTESIAN_POINT ( 'NONE',  ( 15.32816939922342847, -9.740707523384177335, 4.000000000000000000 ) ) ;
#64790=CARTESIAN_POINT ( 'NONE',  ( 51.48921356237309510, -27.52281430457091460, 5.000000000000000000 ) ) ;
#64792=VERTEX_POINT ( 'NONE', #88083 ) ;
#64793=VECTOR ( 'NONE', #15798, 1000.000000000000227 ) ;
#64796=LINE ( 'NONE', #140897, #117197 ) ;
#64797=CARTESIAN_POINT ( 'NONE',  ( 8.999999999999941380, -3.485240976185067563, -4.108735105802378662 ) ) ;
#64798=VECTOR ( 'NONE', #19110, 1000.000000000000114 ) ;
#64799=ADVANCED_FACE ( 'NONE', ( #132327 ), #44619, .F. ) ;
#64800=LINE ( 'NONE', #87967, #13891 ) ;
#64801=LINE ( 'NONE', #98140, #71681 ) ;
#64802=ORIENTED_EDGE ( 'NONE', *, *, #67709, .T. ) ;
#64803=CARTESIAN_POINT ( 'NONE',  ( 0.000000000000000000, 0.000000000000000000, 5.000000000000000000 ) ) ;
#64806=EDGE_CURVE ( 'NONE', #103866, #135194, #122114, .T. ) ;
#64809=EDGE_LOOP ( 'NONE', ( #113669, #21115, #135578, #58889 ) ) ;
#64810=VERTEX_POINT ( 'NONE', #1731 ) ;
#64811=AXIS2_PLACEMENT_3D ( 'NONE', #26047, #36216, #69577 ) ;
#64812=FACE_OUTER_BOUND ( 'NONE', #1001, .T. ) ;
#64813=CARTESIAN_POINT ( 'NONE',  ( 39.29974487139159578, -27.71228299555233576, 4.000000000000000000 ) ) ;
#64814=VERTEX_POINT ( 'NONE', #106584 ) ;
#64816=ORIENTED_EDGE ( 'NONE', *, *, #38651, .T. ) ;
#64818=EDGE_LOOP ( 'NONE', ( #77769, #49103, #126220, #17155 ) ) ;
#64820=DIRECTION ( 'NONE',  ( -0.7071067811865487940, 0.7071067811865463515, 0.000000000000000000 ) ) ;
#64821=DIRECTION ( 'NONE',  ( -0.7071067811865486830, 0.7071067811865464625, 0.000000000000000000 ) ) ;
#64822=VECTOR ( 'NONE', #49557, 1000.000000000000227 ) ;
#64823=EDGE_CURVE ( 'NONE', #126389, #89318, #128386, .T. ) ;
#64824=CARTESIAN_POINT ( 'NONE',  ( 17.99451991528748351, 28.92564299267950645, 4.000000000000000000 ) ) ;
#64825=FACE_BOUND ( 'NONE', #129397, .T. ) ;
#64826=DIRECTION ( 'NONE',  ( -0.000000000000000000, 0.000000000000000000, 1.000000000000000000 ) ) ;
#64828=CARTESIAN_POINT ( 'NONE',  ( -27.29974487139158512, -27.71228299555225405, 4.000000000000000000 ) ) ;
#64830=ORIENTED_EDGE ( 'NONE', *, *, #46400, .T. ) ;
#64831=LINE ( 'NONE', #9706, #78766 ) ;
#64833=VERTEX_POINT ( 'NONE', #16752 ) ;
#64835=ORIENTED_EDGE ( 'NONE', *, *, #114431, .F. ) ;
#64836=EDGE_CURVE ( 'NONE', #97655, #75539, #82054, .T. ) ;
#64837=LINE ( 'NONE', #124201, #360 ) ;
#64838=ORIENTED_EDGE ( 'NONE', *, *, #14501, .T. ) ;
#64839=DIRECTION ( 'NONE',  ( -0.000000000000000000, -0.3543493200069152693, 0.9351131265310292928 ) ) ;
#64840=EDGE_CURVE ( 'NONE', #15605, #45425, #5844, .T. ) ;
#64841=LINE ( 'NONE', #53986, #121264 ) ;
#64842=DIRECTION ( 'NONE',  ( -0.000000000000000000, 0.3543493200069153248, 0.9351131265310292928 ) ) ;
#64843=VECTOR ( 'NONE', #35307, 1000.000000000000000 ) ;
#64845=CARTESIAN_POINT ( 'NONE',  ( 10.49999999999992539, -6.839392718269124316, -8.480912228396110919 ) ) ;
#64846=CARTESIAN_POINT ( 'NONE',  ( 24.29974487139158867, -27.71228299555223273, 4.000000000000000000 ) ) ;
#64848=DIRECTION ( 'NONE',  ( -0.6830127018922181881, 0.6830127018922202975, -0.2588190451025214056 ) ) ;
#64849=AXIS2_PLACEMENT_3D ( 'NONE', #111115, #110404, #34302 ) ;
#64850=ORIENTED_EDGE ( 'NONE', *, *, #19594, .F. ) ;
#64851=VECTOR ( 'NONE', #47951, 1000.000000000000227 ) ;
#64854=AXIS2_PLACEMENT_3D ( 'NONE', #22573, #23299, #11700 ) ;
#64855=ORIENTED_EDGE ( 'NONE', *, *, #79569, .T. ) ;
#64856=CARTESIAN_POINT ( 'NONE',  ( -18.18398860626898994, 28.73617430169800002, 5.000000000000000000 ) ) ;
#64857=LINE ( 'NONE', #62012, #65167 ) ;
#64859=ORIENTED_EDGE ( 'NONE', *, *, #35920, .F. ) ;
#64860=VERTEX_POINT ( 'NONE', #29062 ) ;
#64861=ORIENTED_EDGE ( 'NONE', *, *, #3415, .T. ) ;
#64862=EDGE_CURVE ( 'NONE', #53913, #42124, #49423, .T. ) ;
#64864=ORIENTED_EDGE ( 'NONE', *, *, #93477, .T. ) ;
#64865=VECTOR ( 'NONE', #2668, 1000.000000000000000 ) ;
#64866=LINE ( 'NONE', #54006, #38935 ) ;
#64867=ADVANCED_FACE ( 'NONE', ( #18141 ), #15289, .F. ) ;
#64872=DIRECTION ( 'NONE',  ( -0.6830127018922181881, 0.6830127018922202975, -0.2588190451025214056 ) ) ;
#64874=AXIS2_PLACEMENT_3D ( 'NONE', #109994, #143341, #19422 ) ;
#64875=DIRECTION ( 'NONE',  ( -0.7071067811865486830, -0.7071067811865464625, -0.000000000000000000 ) ) ;
#64876=CARTESIAN_POINT ( 'NONE',  ( 34.49999999999976552, 18.05432934483075513, 4.994342998332162331 ) ) ;
#64877=ORIENTED_EDGE ( 'NONE', *, *, #56875, .F. ) ;
#64878=ORIENTED_EDGE ( 'NONE', *, *, #88313, .F. ) ;
#64879=CARTESIAN_POINT ( 'NONE',  ( 41.99451991528749062, 28.92564299267967343, 4.000000000000000000 ) ) ;
#64881=DIRECTION ( 'NONE',  ( -0.6830127018922180770, -0.6830127018922204085, -0.2588190451025213501 ) ) ;
#64883=VECTOR ( 'NONE', #122159, 999.9999999999998863 ) ;
#64884=ADVANCED_FACE ( 'NONE', ( #105875 ), #40662, .F. ) ;
#64885=CARTESIAN_POINT ( 'NONE',  ( 27.18398860626900060, 28.73617430169806042, 5.000000000000000000 ) ) ;
#64887=ORIENTED_EDGE ( 'NONE', *, *, #4566, .T. ) ;
#64888=VERTEX_POINT ( 'NONE', #51546 ) ;
#64889=VECTOR ( 'NONE', #119976, 1000.000000000000000 ) ;
#64890=CARTESIAN_POINT ( 'NONE',  ( -27.48921356237309155, -27.52281430457074762, 5.000000000000000000 ) ) ;
#64891=DIRECTION ( 'NONE',  ( -0.3543493200069162685, -0.000000000000000000, -0.9351131265310288487 ) ) ;
#64892=DIRECTION ( 'NONE',  ( -0.3543493200069163240, -0.000000000000000000, -0.9351131265310288487 ) ) ;
#64893=VECTOR ( 'NONE', #8705, 1000.000000000000000 ) ;
#64895=DIRECTION ( 'NONE',  ( -0.7071067811865487940, 0.7071067811865463515, -0.000000000000000000 ) ) ;
#64896=CARTESIAN_POINT ( 'NONE',  ( -13.26506670282042499, 12.75929247661558996, 18.34774599283959517 ) ) ;
#64897=FACE_OUTER_BOUND ( 'NONE', #106619, .T. ) ;
#64898=ADVANCED_FACE ( 'NONE', ( #59576 ), #115306, .F. ) ;
#64899=ORIENTED_EDGE ( 'NONE', *, *, #42293, .T. ) ;
#64900=CARTESIAN_POINT ( 'NONE',  ( -29.67183060077627843, -18.74070752338409918, 4.000000000000000000 ) ) ;
#64901=ORIENTED_EDGE ( 'NONE', *, *, #45178, .F. ) ;
#64902=LINE ( 'NONE', #10480, #54050 ) ;
#64903=CARTESIAN_POINT ( 'NONE',  ( 34.92499999999999005, 21.66246187583879390, 4.000000000000000000 ) ) ;
#64904=VERTEX_POINT ( 'NONE', #71882 ) ;
#64906=CARTESIAN_POINT ( 'NONE',  ( -9.489213562373095101, -27.52281430457062328, 5.000000000000000000 ) ) ;
#64907=FACE_OUTER_BOUND ( 'NONE', #11865, .T. ) ;
#64908=ORIENTED_EDGE ( 'NONE', *, *, #18942, .F. ) ;
#64909=ORIENTED_EDGE ( 'NONE', *, *, #20444, .F. ) ;
#64910=CARTESIAN_POINT ( 'NONE',  ( 0.000000000000000000, 0.000000000000000000, 5.000000000000000000 ) ) ;
#64912=VECTOR ( 'NONE', #37286, 1000.000000000000227 ) ;
#64913=FACE_OUTER_BOUND ( 'NONE', #34188, .T. ) ;
#64914=DIRECTION ( 'NONE',  ( 0.7071067811865486830, -0.7071067811865464625, -0.000000000000000000 ) ) ;
#64916=CARTESIAN_POINT ( 'NONE',  ( -39.18398860626899705, 28.73617430169814568, 5.000000000000000000 ) ) ;
#64919=ORIENTED_EDGE ( 'NONE', *, *, #12188, .T. ) ;
#64920=DIRECTION ( 'NONE',  ( -0.000000000000000000, -0.3543493200069152693, 0.9351131265310292928 ) ) ;
#64921=EDGE_CURVE ( 'NONE', #137344, #104855, #60288, .T. ) ;
#64922=ORIENTED_EDGE ( 'NONE', *, *, #5022, .T. ) ;
#64923=VECTOR ( 'NONE', #64505, 1000.000000000000227 ) ;
#64925=ORIENTED_EDGE ( 'NONE', *, *, #68566, .F. ) ;
#64926=LINE ( 'NONE', #87388, #117827 ) ;
#64927=PLANE ( 'NONE',  #116041 ) ;
#64929=FACE_OUTER_BOUND ( 'NONE', #8305, .T. ) ;
#64930=CARTESIAN_POINT ( 'NONE',  ( -20.99999999999985434, -13.97847968911261951, -0.1324546996127294596 ) ) ;
#64931=CARTESIAN_POINT ( 'NONE',  ( 19.56687199751245032, -21.74070752338406720, 6.915939825044026712 ) ) ;
#64932=EDGE_CURVE ( 'NONE', #38574, #90775, #116054, .T. ) ;
#64933=ADVANCED_FACE ( 'NONE', ( #50823 ), #105184, .F. ) ;
#64934=ORIENTED_EDGE ( 'NONE', *, *, #57775, .T. ) ;
#64935=ORIENTED_EDGE ( 'NONE', *, *, #42660, .F. ) ;
#64937=DIRECTION ( 'NONE',  ( 0.3543493200069162685, -0.000000000000000000, -0.9351131265310288487 ) ) ;
#64938=VECTOR ( 'NONE', #32299, 1000.000000000000000 ) ;
#64939=DIRECTION ( 'NONE',  ( -0.7071067811865487940, 0.7071067811865463515, 0.000000000000000000 ) ) ;
#64940=CARTESIAN_POINT ( 'NONE',  ( -0.7123099396602794453, -21.73547319004781642, 4.999917730833664642 ) ) ;
#64941=EDGE_CURVE ( 'NONE', #142188, #51446, #138545, .T. ) ;
#64943=EDGE_CURVE ( 'NONE', #44540, #128760, #139281, .T. ) ;
#64944=DIRECTION ( 'NONE',  ( -0.6830127018922181881, 0.6830127018922202975, -0.2588190451025214056 ) ) ;
#64945=DIRECTION ( 'NONE',  ( -0.000000000000000000, -0.3543493200069152693, 0.9351131265310292928 ) ) ;
#64946=ORIENTED_EDGE ( 'NONE', *, *, #47383, .T. ) ;
#64949=DIRECTION ( 'NONE',  ( -0.7071067811865486830, -0.7071067811865464625, 0.000000000000000000 ) ) ;
#64950=EDGE_CURVE ( 'NONE', #73748, #109110, #84191, .T. ) ;
#64951=LINE ( 'NONE', #64226, #134136 ) ;
#64952=LINE ( 'NONE', #106996, #35929 ) ;
#64953=EDGE_CURVE ( 'NONE', #76469, #65412, #92883, .T. ) ;
#64954=ORIENTED_EDGE ( 'NONE', *, *, #103897, .F. ) ;
#64955=VECTOR ( 'NONE', #54760, 1000.000000000000000 ) ;
#64956=LINE ( 'NONE', #87415, #51395 ) ;
#64959=VERTEX_POINT ( 'NONE', #10843 ) ;
#64962=LINE ( 'NONE', #40365, #70935 ) ;
#64964=ORIENTED_EDGE ( 'NONE', *, *, #70482, .F. ) ;
#64965=AXIS2_PLACEMENT_3D ( 'NONE', #54377, #131186, #111572 ) ;
#64966=VECTOR ( 'NONE', #51196, 1000.000000000000227 ) ;
#64967=AXIS2_PLACEMENT_3D ( 'NONE', #72416, #124608, #141937 ) ;
#64969=AXIS2_PLACEMENT_3D ( 'NONE', #53812, #42934, #76265 ) ;
#64970=ADVANCED_FACE ( 'NONE', ( #108011 ), #9404, .F. ) ;
#64971=CARTESIAN_POINT ( 'NONE',  ( -10.49999999999992539, 10.46639925780214853, 5.000000000000000000 ) ) ;
#64972=DIRECTION ( 'NONE',  ( 0.7071067811865487940, 0.7071067811865463515, 0.000000000000000000 ) ) ;
#64974=LINE ( 'NONE', #99709, #3534 ) ;
#64975=VERTEX_POINT ( 'NONE', #42816 ) ;
#64976=LINE ( 'NONE', #19307, #113185 ) ;
#64977=DIRECTION ( 'NONE',  ( 0.3543493200069162685, -0.000000000000000000, -0.9351131265310288487 ) ) ;
#64978=CARTESIAN_POINT ( 'NONE',  ( -30.13499573751603933, 3.759292476615678336, 15.36553568819732796 ) ) ;
#64980=EDGE_CURVE ( 'NONE', #48229, #107272, #110167, .T. ) ;
#64981=DIRECTION ( 'NONE',  ( 0.7071067811865486830, -0.7071067811865464625, -0.000000000000000000 ) ) ;
#64982=ORIENTED_EDGE ( 'NONE', *, *, #100451, .F. ) ;
#64983=ORIENTED_EDGE ( 'NONE', *, *, #34196, .T. ) ;
#64985=ORIENTED_EDGE ( 'NONE', *, *, #58671, .T. ) ;
#64986=DIRECTION ( 'NONE',  ( -0.7071067811865487940, 0.7071067811865463515, -0.000000000000000000 ) ) ;
#64989=CARTESIAN_POINT ( 'NONE',  ( -57.29974487139158157, -27.71228299555246011, 4.000000000000000000 ) ) ;
#64990=CARTESIAN_POINT ( 'NONE',  ( -12.18398860626900060, 28.73617430169795739, 5.000000000000000000 ) ) ;
#64991=ORIENTED_EDGE ( 'NONE', *, *, #56498, .T. ) ;
#64992=CARTESIAN_POINT ( 'NONE',  ( -38.99451991528749062, 28.92564299267965211, 4.000000000000000000 ) ) ;
#64993=AXIS2_PLACEMENT_3D ( 'NONE', #41420, #63227, #140724 ) ;
#64994=EDGE_CURVE ( 'NONE', #73333, #98820, #142130, .T. ) ;
#64996=AXIS2_PLACEMENT_3D ( 'NONE', #13985, #102473, #12571 ) ;
#64997=LINE ( 'NONE', #86743, #44518 ) ;
#64998=EDGE_CURVE ( 'NONE', #67140, #28687, #99283, .T. ) ;
#64999=VECTOR ( 'NONE', #84224, 1000.000000000000000 ) ;
#65000=PLANE ( 'NONE',  #70991 ) ;
#65001=PLANE ( 'NONE',  #21540 ) ;
#65002=VECTOR ( 'NONE', #46775, 1000.000000000000227 ) ;
#65003=ADVANCED_FACE ( 'NONE', ( #42104 ), #19605, .F. ) ;
#65006=LINE ( 'NONE', #9117, #17532 ) ;
#65008=DIRECTION ( 'NONE',  ( 0.6830127018922181881, 0.6830127018922202975, -0.2588190451025214056 ) ) ;
#65009=LINE ( 'NONE', #141855, #9529 ) ;
#65010=FACE_OUTER_BOUND ( 'NONE', #132769, .T. ) ;
#65011=CARTESIAN_POINT ( 'NONE',  ( 18.29974487139159223, -27.71228299555219010, 4.000000000000000000 ) ) ;
#65012=LINE ( 'NONE', #20756, #95192 ) ;
#65013=ORIENTED_EDGE ( 'NONE', *, *, #79328, .T. ) ;
#65014=VECTOR ( 'NONE', #98078, 999.9999999999998863 ) ;
#65015=VERTEX_POINT ( 'NONE', #97891 ) ;
#65017=ORIENTED_EDGE ( 'NONE', *, *, #94829, .T. ) ;
#65018=EDGE_CURVE ( 'NONE', #109272, #43579, #107326, .T. ) ;
#65019=ORIENTED_EDGE ( 'NONE', *, *, #138766, .F. ) ;
#65022=CARTESIAN_POINT ( 'NONE',  ( 34.92499999999998295, 22.22500000000000142, 4.000000000000000000 ) ) ;
#65023=ORIENTED_EDGE ( 'NONE', *, *, #85655, .T. ) ;
#65026=EDGE_CURVE ( 'NONE', #56703, #99523, #30501, .T. ) ;
#65029=VECTOR ( 'NONE', #22229, 1000.000000000000227 ) ;
#65030=DIRECTION ( 'NONE',  ( 0.6830127018922180770, -0.6830127018922204085, -0.2588190451025213501 ) ) ;
#65031=ORIENTED_EDGE ( 'NONE', *, *, #30145, .F. ) ;
#65032=CARTESIAN_POINT ( 'NONE',  ( 0.000000000000000000, 0.000000000000000000, 5.000000000000000000 ) ) ;
#65034=ORIENTED_EDGE ( 'NONE', *, *, #35835, .T. ) ;
#65036=ORIENTED_EDGE ( 'NONE', *, *, #126582, .T. ) ;
#65040=ORIENTED_EDGE ( 'NONE', *, *, #17658, .F. ) ;
#65041=VECTOR ( 'NONE', #86987, 999.9999999999998863 ) ;
#65042=DIRECTION ( 'NONE',  ( -0.7071067811865486830, -0.7071067811865464625, -0.000000000000000000 ) ) ;
#65043=EDGE_CURVE ( 'NONE', #64534, #2906, #98589, .T. ) ;
#65046=CARTESIAN_POINT ( 'NONE',  ( 18.48921356237309510, -27.52281430457068367, 5.000000000000000000 ) ) ;
#65049=ORIENTED_EDGE ( 'NONE', *, *, #44256, .F. ) ;
#65050=DIRECTION ( 'NONE',  ( 0.000000000000000000, -1.000000000000000000, 0.000000000000000000 ) ) ;
#65052=CARTESIAN_POINT ( 'NONE',  ( 2.510786437626908008, -27.52281430457053446, 5.000000000000000000 ) ) ;
#65053=ADVANCED_FACE ( 'NONE', ( #97126 ), #64543, .T. ) ;
#65054=CARTESIAN_POINT ( 'NONE',  ( -10.17183060077639745, 3.759292476615674783, 4.000000000000000000 ) ) ;
#65055=AXIS2_PLACEMENT_3D ( 'NONE', #92619, #5603, #16480 ) ;
#65056=DIRECTION ( 'NONE',  ( -0.000000000000000000, 0.000000000000000000, 1.000000000000000000 ) ) ;
#65057=VECTOR ( 'NONE', #82464, 1000.000000000000000 ) ;
#65058=ORIENTED_EDGE ( 'NONE', *, *, #85371, .T. ) ;
#65060=FACE_OUTER_BOUND ( 'NONE', #75366, .T. ) ;
#65062=VERTEX_POINT ( 'NONE', #41348 ) ;
#65063=ORIENTED_EDGE ( 'NONE', *, *, #17637, .F. ) ;
#65066=VECTOR ( 'NONE', #77255, 1000.000000000000000 ) ;
#65067=EDGE_LOOP ( 'NONE', ( #71920, #81021, #70135, #69146 ) ) ;
#65068=VECTOR ( 'NONE', #128722, 1000.000000000000000 ) ;
#65070=DIRECTION ( 'NONE',  ( -0.7071067811865486830, -0.7071067811865464625, 0.000000000000000000 ) ) ;
#65071=FACE_OUTER_BOUND ( 'NONE', #103179, .T. ) ;
#65072=EDGE_CURVE ( 'NONE', #98060, #43787, #118914, .T. ) ;
#65073=ORIENTED_EDGE ( 'NONE', *, *, #128356, .T. ) ;
#65074=FACE_OUTER_BOUND ( 'NONE', #35099, .T. ) ;
#65075=VECTOR ( 'NONE', #41774, 999.9999999999998863 ) ;
#65076=ORIENTED_EDGE ( 'NONE', *, *, #33616, .F. ) ;
#65079=DIRECTION ( 'NONE',  ( -0.7071067811865487940, 0.7071067811865463515, -0.000000000000000000 ) ) ;
#65080=AXIS2_PLACEMENT_3D ( 'NONE', #66951, #136471, #69837 ) ;
#65081=DIRECTION ( 'NONE',  ( -0.7071067811865487940, 0.7071067811865463515, 0.000000000000000000 ) ) ;
#65082=VERTEX_POINT ( 'NONE', #52925 ) ;
#65083=ORIENTED_EDGE ( 'NONE', *, *, #81192, .F. ) ;
#65084=VERTEX_POINT ( 'NONE', #86314 ) ;
#65086=AXIS2_PLACEMENT_3D ( 'NONE', #22097, #68507, #57623 ) ;
#65088=CARTESIAN_POINT ( 'NONE',  ( -31.63753812416075206, 22.22499999999999432, 4.000000000000000000 ) ) ;
#65089=PLANE ( 'NONE',  #122365 ) ;
#65090=FACE_OUTER_BOUND ( 'NONE', #119165, .T. ) ;
#65091=VECTOR ( 'NONE', #63391, 1000.000000000000227 ) ;
#65092=PLANE ( 'NONE',  #136379 ) ;
#65094=DIRECTION ( 'NONE',  ( -0.000000000000000000, 0.000000000000000000, 1.000000000000000000 ) ) ;
#65095=PLANE ( 'NONE',  #111452 ) ;
#65097=ORIENTED_EDGE ( 'NONE', *, *, #96182, .F. ) ;
#65098=CARTESIAN_POINT ( 'NONE',  ( 28.49999999999980105, -11.94781430457070392, 5.000000000000000000 ) ) ;
#65099=EDGE_CURVE ( 'NONE', #116519, #43439, #31918, .T. ) ;
#65100=VERTEX_POINT ( 'NONE', #108725 ) ;
#65101=CARTESIAN_POINT ( 'NONE',  ( -21.62762920772360786, 8.558752285115851066, 4.000000000000000000 ) ) ;
#65103=ORIENTED_EDGE ( 'NONE', *, *, #143188, .F. ) ;
#65104=CARTESIAN_POINT ( 'NONE',  ( -17.99451991528748351, 28.92564299267950645, 4.000000000000000000 ) ) ;
#65105=DIRECTION ( 'NONE',  ( -0.000000000000000000, 0.000000000000000000, 1.000000000000000000 ) ) ;
#65106=ORIENTED_EDGE ( 'NONE', *, *, #72494, .T. ) ;
#65107=VECTOR ( 'NONE', #8167, 1000.000000000000000 ) ;
#65108=FACE_OUTER_BOUND ( 'NONE', #63921, .T. ) ;
#65109=ORIENTED_EDGE ( 'NONE', *, *, #33126, .T. ) ;
#65110=FACE_OUTER_BOUND ( 'NONE', #113655, .T. ) ;
#65111=ORIENTED_EDGE ( 'NONE', *, *, #125455, .T. ) ;
#65112=DIRECTION ( 'NONE',  ( -0.000000000000000000, -0.000000000000000000, 1.000000000000000000 ) ) ;
#65114=ORIENTED_EDGE ( 'NONE', *, *, #42860, .F. ) ;
#65116=ADVANCED_FACE ( 'NONE', ( #10152 ), #142819, .F. ) ;
#65118=AXIS2_PLACEMENT_3D ( 'NONE', #40403, #84612, #30211 ) ;
#65120=EDGE_CURVE ( 'NONE', #69350, #59049, #110866, .T. ) ;
#65121=LINE ( 'NONE', #62983, #118591 ) ;
#65122=LINE ( 'NONE', #32478, #137599 ) ;
#65123=EDGE_CURVE ( 'NONE', #111265, #117852, #80439, .T. ) ;
#65124=CARTESIAN_POINT ( 'NONE',  ( -25.49999999999981526, -11.56887692260769995, 4.000000000000000000 ) ) ;
#65126=VECTOR ( 'NONE', #126609, 1000.000000000000000 ) ;
#65129=FACE_OUTER_BOUND ( 'NONE', #132962, .T. ) ;
#65130=ADVANCED_FACE ( 'NONE', ( #56578 ), #133387, .F. ) ;
#65131=VERTEX_POINT ( 'NONE', #34076 ) ;
#65132=EDGE_LOOP ( 'NONE', ( #49935, #55062, #33832, #120960 ) ) ;
#65133=CARTESIAN_POINT ( 'NONE',  ( -5.999999999999963585, 11.58746187583913390, 4.000000000000000000 ) ) ;
#65134=ORIENTED_EDGE ( 'NONE', *, *, #138064, .F. ) ;
#65135=EDGE_CURVE ( 'NONE', #110737, #84831, #78288, .T. ) ;
#65136=DIRECTION ( 'NONE',  ( -0.3543493200069162685, -0.000000000000000000, -0.9351131265310288487 ) ) ;
#65137=FACE_OUTER_BOUND ( 'NONE', #139908, .T. ) ;
#65138=AXIS2_PLACEMENT_3D ( 'NONE', #1383, #132688, #65996 ) ;
#65139=DIRECTION ( 'NONE',  ( 0.7071067811865487940, -0.7071067811865463515, 0.000000000000000000 ) ) ;
#65140=VERTEX_POINT ( 'NONE', #135527 ) ;
#65141=DIRECTION ( 'NONE',  ( -0.7071067811865487940, 0.7071067811865463515, -0.000000000000000000 ) ) ;
#65142=CARTESIAN_POINT ( 'NONE',  ( 75.48921356237309510, -27.52281430457107803, 5.000000000000000000 ) ) ;
#65143=EDGE_CURVE ( 'NONE', #108859, #59468, #22435, .T. ) ;
#65145=CARTESIAN_POINT ( 'NONE',  ( 10.49999999999993250, 6.052185695429105117, 5.000000000000000000 ) ) ;
#65147=CARTESIAN_POINT ( 'NONE',  ( 34.92499999999998295, -8.993876922607942248, 4.000000000000000000 ) ) ;
#65148=ORIENTED_EDGE ( 'NONE', *, *, #70201, .T. ) ;
#65151=VECTOR ( 'NONE', #94340, 1000.000000000000000 ) ;
#65152=LINE ( 'NONE', #19474, #125776 ) ;
#65153=CARTESIAN_POINT ( 'NONE',  ( 45.18398860626900415, 28.73617430169818832, 5.000000000000000000 ) ) ;
#65156=VERTEX_POINT ( 'NONE', #33387 ) ;
#65158=ORIENTED_EDGE ( 'NONE', *, *, #53861, .T. ) ;
#65161=CARTESIAN_POINT ( 'NONE',  ( 21.41161490594815930, 22.22500000000000142, 4.777194822843818578 ) ) ;
#65163=ORIENTED_EDGE ( 'NONE', *, *, #49468, .F. ) ;
#65164=AXIS2_PLACEMENT_3D ( 'NONE', #39021, #70279, #83245 ) ;
#65166=DIRECTION ( 'NONE',  ( -0.3543493200069162685, -0.000000000000000000, -0.9351131265310288487 ) ) ;
#65167=VECTOR ( 'NONE', #86614, 1000.000000000000000 ) ;
#65170=VERTEX_POINT ( 'NONE', #77588 ) ;
#65171=LINE ( 'NONE', #99165, #39741 ) ;
#65172=EDGE_CURVE ( 'NONE', #113402, #141378, #111579, .T. ) ;
#65173=VECTOR ( 'NONE', #123926, 999.9999999999998863 ) ;
#65175=CARTESIAN_POINT ( 'NONE',  ( -34.49999999999975842, 12.05432934483081553, 4.994342998332167660 ) ) ;
#65176=ORIENTED_EDGE ( 'NONE', *, *, #142876, .F. ) ;
#65177=VERTEX_POINT ( 'NONE', #44988 ) ;
#65178=EDGE_LOOP ( 'NONE', ( #52546, #77233, #4666, #136863 ) ) ;
#65179=CARTESIAN_POINT ( 'NONE',  ( 7.499999999999944045, -2.568876922607782998, 4.000000000000000000 ) ) ;
#65180=FACE_OUTER_BOUND ( 'NONE', #61277, .T. ) ;
#65182=CARTESIAN_POINT ( 'NONE',  ( 17.20710678118642889, 12.75929247661558463, 5.000000000000000000 ) ) ;
#65183=VECTOR ( 'NONE', #110394, 1000.000000000000227 ) ;
#65186=DIRECTION ( 'NONE',  ( -0.000000000000000000, -0.3543493200069152693, 0.9351131265310292928 ) ) ;
#65187=PRESENTATION_STYLE_ASSIGNMENT (( #86922 ) ) ;
#65189=ORIENTED_EDGE ( 'NONE', *, *, #59560, .T. ) ;
#65190=AXIS2_PLACEMENT_3D ( 'NONE', #15905, #6448, #60191 ) ;
#65192=EDGE_CURVE ( 'NONE', #105061, #31469, #89160, .T. ) ;
#65193=ORIENTED_EDGE ( 'NONE', *, *, #97046, .F. ) ;
#65194=EDGE_LOOP ( 'NONE', ( #22387, #104487, #68304, #15742 ) ) ;
#65195=AXIS2_PLACEMENT_3D ( 'NONE', #132051, #135609, #112425 ) ;
#65196=VECTOR ( 'NONE', #57874, 1000.000000000000000 ) ;
#65197=PLANE ( 'NONE',  #84462 ) ;
#65200=DIRECTION ( 'NONE',  ( 0.3543493200069162685, -0.000000000000000000, -0.9351131265310288487 ) ) ;
#65201=EDGE_CURVE ( 'NONE', #133459, #93212, #138366, .T. ) ;
#65202=AXIS2_PLACEMENT_3D ( 'NONE', #21165, #75560, #74869 ) ;
#65203=LINE ( 'NONE', #121672, #87282 ) ;
#65204=LINE ( 'NONE', #55743, #69211 ) ;
#65205=VECTOR ( 'NONE', #93452, 1000.000000000000000 ) ;
#65208=CARTESIAN_POINT ( 'NONE',  ( 25.49999999999982947, 0.05218569542917231296, 5.000000000000000000 ) ) ;
#65209=EDGE_LOOP ( 'NONE', ( #16023, #102595, #15959, #77039 ) ) ;
#65210=DIRECTION ( 'NONE',  ( -0.000000000000000000, 0.3543493200069153248, 0.9351131265310292928 ) ) ;
#65212=EDGE_LOOP ( 'NONE', ( #120692, #53253, #8429, #62564 ) ) ;
#65215=ORIENTED_EDGE ( 'NONE', *, *, #103404, .T. ) ;
#65217=FACE_OUTER_BOUND ( 'NONE', #59485, .T. ) ;
#65219=EDGE_LOOP ( 'NONE', ( #24782, #515, #50458, #142054 ) ) ;
#65220=ORIENTED_EDGE ( 'NONE', *, *, #140747, .T. ) ;
#65221=CARTESIAN_POINT ( 'NONE',  ( -2.816011393730999401, 28.73617430169785436, 5.000000000000000000 ) ) ;
#65222=LINE ( 'NONE', #63084, #117732 ) ;
#65223=LINE ( 'NONE', #10088, #65750 ) ;
#65225=DIRECTION ( 'NONE',  ( 0.6830127018922181881, 0.6830127018922202975, -0.2588190451025214056 ) ) ;
#65227=CARTESIAN_POINT ( 'NONE',  ( 51.18398860626899705, 28.73617430169823095, 5.000000000000000000 ) ) ;
#65228=CARTESIAN_POINT ( 'NONE',  ( -30.48921356237309510, -27.52281430457076894, 5.000000000000000000 ) ) ;
#65229=VECTOR ( 'NONE', #29760, 1000.000000000000000 ) ;
#65230=DIRECTION ( 'NONE',  ( 0.000000000000000000, -1.000000000000000000, 0.000000000000000000 ) ) ;
#65231=ADVANCED_FACE ( 'NONE', ( #73131 ), #49244, .F. ) ;
#65232=DIRECTION ( 'NONE',  ( 0.3543493200069162685, -0.000000000000000000, -0.9351131265310288487 ) ) ;
#65233=ADVANCED_FACE ( 'NONE', ( #49946 ), #116609, .F. ) ;
#65235=DIRECTION ( 'NONE',  ( -0.7071067811865486830, -0.7071067811865464625, 0.000000000000000000 ) ) ;
#65236=AXIS2_PLACEMENT_3D ( 'NONE', #125293, #47769, #114407 ) ;
#65237=VERTEX_POINT ( 'NONE', #61553 ) ;
#65238=ORIENTED_EDGE ( 'NONE', *, *, #10366, .T. ) ;
#65239=ORIENTED_EDGE ( 'NONE', *, *, #60800, .F. ) ;
#65240=LINE ( 'NONE', #109425, #125948 ) ;
#65241=EDGE_LOOP ( 'NONE', ( #1874, #119300, #119668, #108424 ) ) ;
#65242=VERTEX_POINT ( 'NONE', #91996 ) ;
#65243=LINE ( 'NONE', #109428, #49154 ) ;
#65244=LINE ( 'NONE', #141341, #52472 ) ;
#65245=ADVANCED_FACE ( 'NONE', ( #28181 ), #17289, .T. ) ;
#65247=LINE ( 'NONE', #142776, #108883 ) ;
#65248=ORIENTED_EDGE ( 'NONE', *, *, #19905, .F. ) ;
#65249=DIRECTION ( 'NONE',  ( -0.7071067811865486830, 0.7071067811865464625, 0.000000000000000000 ) ) ;
#65250=VECTOR ( 'NONE', #74746, 999.9999999999998863 ) ;
#65251=VERTEX_POINT ( 'NONE', #105701 ) ;
#65252=DIRECTION ( 'NONE',  ( -0.7071067811865487940, 0.7071067811865463515, 0.000000000000000000 ) ) ;
#65253=CARTESIAN_POINT ( 'NONE',  ( 27.70710678118635784, -18.74070752338408852, 5.000000000000000000 ) ) ;
#65255=ORIENTED_EDGE ( 'NONE', *, *, #62906, .T. ) ;
#65257=LINE ( 'NONE', #99249, #20426 ) ;
#65258=CARTESIAN_POINT ( 'NONE',  ( -27.81246187583927920, -22.22500000000000142, 4.000000000000000000 ) ) ;
#65259=CARTESIAN_POINT ( 'NONE',  ( -27.72281430457040940, -21.72500000000000142, 5.000000000000000000 ) ) ;
#65260=VERTEX_POINT ( 'NONE', #39049 ) ;
#65261=ORIENTED_EDGE ( 'NONE', *, *, #29552, .F. ) ;
#65262=ORIENTED_EDGE ( 'NONE', *, *, #118769, .T. ) ;
#65263=DIRECTION ( 'NONE',  ( 0.6830127018922181881, 0.6830127018922202975, -0.2588190451025214056 ) ) ;
#65264=VECTOR ( 'NONE', #123015, 1000.000000000000227 ) ;
#65266=CARTESIAN_POINT ( 'NONE',  ( -21.18398860626899349, 28.73617430169802134, 5.000000000000000000 ) ) ;
#65267=CARTESIAN_POINT ( 'NONE',  ( -26.95341186370439601, 14.25929247661557042, 18.84478104361334161 ) ) ;
#65268=EDGE_CURVE ( 'NONE', #103666, #42327, #50639, .T. ) ;
#65269=( BOUNDED_CURVE ( )  B_SPLINE_CURVE ( 3, ( #21771, #44258, #99299, #88471 ),
 .UNSPECIFIED., .F., .F. ) 
 B_SPLINE_CURVE_WITH_KNOTS ( ( 4, 4 ),
 ( 4.628641526727098388, 4.642507259593577018 ),
 .UNSPECIFIED. ) 
 CURVE ( )  GEOMETRIC_REPRESENTATION_ITEM ( )  RATIONAL_B_SPLINE_CURVE ( ( 1.000000000000000000, 0.9999839785185119512, 0.9999839785185119512, 1.000000000000000000 ) ) 
 REPRESENTATION_ITEM ( '' )  );
#65270=ORIENTED_EDGE ( 'NONE', *, *, #118073, .T. ) ;
#65273=VECTOR ( 'NONE', #27723, 999.9999999999998863 ) ;
#65274=DIRECTION ( 'NONE',  ( 0.7071067811865487940, -0.7071067811865463515, 0.000000000000000000 ) ) ;
#65275=ORIENTED_EDGE ( 'NONE', *, *, #36949, .F. ) ;
#65276=DIRECTION ( 'NONE',  ( 0.3543493200069162685, -0.000000000000000000, -0.9351131265310288487 ) ) ;
#65277=AXIS2_PLACEMENT_3D ( 'NONE', #30902, #119299, #19984 ) ;
#65278=VECTOR ( 'NONE', #18524, 1000.000000000000000 ) ;
#65280=CARTESIAN_POINT ( 'NONE',  ( -9.183988606268997046, 28.73617430169793607, 5.000000000000000000 ) ) ;
#65281=ORIENTED_EDGE ( 'NONE', *, *, #81633, .F. ) ;
#65282=CARTESIAN_POINT ( 'NONE',  ( 16.73493329717938494, 12.75929247661558996, 18.34774599283952412 ) ) ;
#65284=ORIENTED_EDGE ( 'NONE', *, *, #67451, .T. ) ;
#65285=DIRECTION ( 'NONE',  ( -0.000000000000000000, 0.000000000000000000, 1.000000000000000000 ) ) ;
#65287=CARTESIAN_POINT ( 'NONE',  ( 69.18398860626899705, 28.73617430169835529, 5.000000000000000000 ) ) ;
#65289=CARTESIAN_POINT ( 'NONE',  ( 39.18398860626899705, 28.73617430169814568, 5.000000000000000000 ) ) ;
#65290=DIRECTION ( 'NONE',  ( -0.7071067811865486830, -0.7071067811865464625, 0.000000000000000000 ) ) ;
#65293=CARTESIAN_POINT ( 'NONE',  ( -32.99999999999976552, 8.587461875839160541, 4.000000000000000000 ) ) ;
#65294=ADVANCED_FACE ( 'NONE', ( #16562 ), #60853, .F. ) ;
#65296=CARTESIAN_POINT ( 'NONE',  ( 28.49999999999980815, 9.052185695429077583, 5.000000000000000000 ) ) ;
#65297=CARTESIAN_POINT ( 'NONE',  ( 48.48921356237309510, -27.52281430457089328, 5.000000000000000000 ) ) ;
#65298=DIRECTION ( 'NONE',  ( -0.7071067811865486830, -0.7071067811865464625, -0.000000000000000000 ) ) ;
#65299=DIRECTION ( 'NONE',  ( 0.7071067811865487940, 0.7071067811865463515, 0.000000000000000000 ) ) ;
#65300=DIRECTION ( 'NONE',  ( 0.6830127018922181881, 0.6830127018922202975, -0.2588190451025214056 ) ) ;
#65301=LINE ( 'NONE', #64556, #27498 ) ;
#65302=CARTESIAN_POINT ( 'NONE',  ( -1.998069433179001653, -22.22500000000000142, 4.500000000000000888 ) ) ;
#65303=CARTESIAN_POINT ( 'NONE',  ( -45.18398860626900415, 28.73617430169818832, 5.000000000000000000 ) ) ;
#65304=EDGE_CURVE ( 'NONE', #57105, #66501, #94826, .T. ) ;
#65305=EDGE_LOOP ( 'NONE', ( #67285, #90050, #37074, #45509 ) ) ;
#65306=EDGE_CURVE ( 'NONE', #37520, #126076, #92702, .T. ) ;
#65307=VECTOR ( 'NONE', #78046, 1000.000000000000000 ) ;
#65309=ORIENTED_EDGE ( 'NONE', *, *, #23737, .T. ) ;
#65311=VECTOR ( 'NONE', #113454, 999.9999999999998863 ) ;
#65312=ORIENTED_EDGE ( 'NONE', *, *, #102066, .F. ) ;
#65314=AXIS2_PLACEMENT_3D ( 'NONE', #85513, #139232, #62381 ) ;
#65316=DIRECTION ( 'NONE',  ( 0.3543493200069162685, -0.000000000000000000, -0.9351131265310288487 ) ) ;
#65318=VECTOR ( 'NONE', #136425, 1000.000000000000000 ) ;
#65319=ORIENTED_EDGE ( 'NONE', *, *, #102066, .T. ) ;
#65320=CARTESIAN_POINT ( 'NONE',  ( 23.99999999999983302, 20.96639925780204550, 5.000000000000000000 ) ) ;
#65322=ADVANCED_FACE ( 'NONE', ( #26743 ), #139091, .T. ) ;
#65323=LINE ( 'NONE', #98618, #30176 ) ;
#65324=FACE_OUTER_BOUND ( 'NONE', #137110, .T. ) ;
#65325=EDGE_LOOP ( 'NONE', ( #15308, #32469, #50044, #132250 ) ) ;
#65326=ADVANCED_FACE ( 'NONE', ( #9223 ), #75966, .F. ) ;
#65328=PLANE ( 'NONE',  #33512 ) ;
#65329=DIRECTION ( 'NONE',  ( -0.7071067811865486830, -0.7071067811865464625, -0.000000000000000000 ) ) ;
#65331=VECTOR ( 'NONE', #110444, 1000.000000000000000 ) ;
#65333=DIRECTION ( 'NONE',  ( -0.7071067811865486830, -0.7071067811865464625, -0.000000000000000000 ) ) ;
#65335=EDGE_CURVE ( 'NONE', #32425, #131572, #131060, .T. ) ;
#65336=LINE ( 'NONE', #89896, #63140 ) ;
#65337=VERTEX_POINT ( 'NONE', #120139 ) ;
#65338=ORIENTED_EDGE ( 'NONE', *, *, #100318, .F. ) ;
#65340=ORIENTED_EDGE ( 'NONE', *, *, #107225, .T. ) ;
#65341=DIRECTION ( 'NONE',  ( 0.7071067811865487940, -0.7071067811865463515, 0.000000000000000000 ) ) ;
#65342=AXIS2_PLACEMENT_3D ( 'NONE', #13049, #82614, #49301 ) ;
#65343=CARTESIAN_POINT ( 'NONE',  ( -21.32816939922338406, -9.740707523384182664, 4.000000000000000000 ) ) ;
#65344=EDGE_CURVE ( 'NONE', #40790, #143444, #53503, .T. ) ;
#65345=AXIS2_PLACEMENT_3D ( 'NONE', #52768, #118002, #20140 ) ;
#65346=CARTESIAN_POINT ( 'NONE',  ( 3.046588136295422355, 14.25929247661557042, 18.84478104361327055 ) ) ;
#65348=FACE_OUTER_BOUND ( 'NONE', #5722, .T. ) ;
#65349=CARTESIAN_POINT ( 'NONE',  ( -10.00193056682090997, -22.22500000000000142, 4.500000000000000888 ) ) ;
#65351=ORIENTED_EDGE ( 'NONE', *, *, #82209, .F. ) ;
#65352=VERTEX_POINT ( 'NONE', #31747 ) ;
#65353=EDGE_CURVE ( 'NONE', #6537, #72772, #51370, .T. ) ;
#65355=LINE ( 'NONE', #21814, #50817 ) ;
#65356=CARTESIAN_POINT ( 'NONE',  ( 24.70710678118637560, -15.74070752338411339, 5.000000000000000000 ) ) ;
#65360=CARTESIAN_POINT ( 'NONE',  ( 0.000000000000000000, 0.000000000000000000, 5.000000000000000000 ) ) ;
#65361=CARTESIAN_POINT ( 'NONE',  ( 34.92499999999998295, 3.207916084809844914, -2.206283991393068966 ) ) ;
#65362=EDGE_CURVE ( 'NONE', #124820, #6035, #99918, .T. ) ;
#65363=CARTESIAN_POINT ( 'NONE',  ( 7.637538124160930586, 22.22500000000000142, 4.000000000000000000 ) ) ;
#65364=VECTOR ( 'NONE', #75639, 999.9999999999998863 ) ;
#65365=EDGE_CURVE ( 'NONE', #70306, #126386, #141205, .T. ) ;
#65368=LINE ( 'NONE', #109547, #78020 ) ;
#65369=ORIENTED_EDGE ( 'NONE', *, *, #47815, .F. ) ;
#65370=VERTEX_POINT ( 'NONE', #52762 ) ;
#65371=AXIS2_PLACEMENT_3D ( 'NONE', #44616, #111227, #11919 ) ;
#65372=AXIS2_PLACEMENT_3D ( 'NONE', #96745, #70952, #40986 ) ;
#65373=ORIENTED_EDGE ( 'NONE', *, *, #80644, .F. ) ;
#65376=DIRECTION ( 'NONE',  ( -0.6830127018922181881, 0.6830127018922202975, -0.2588190451025214056 ) ) ;
#65377=ORIENTED_EDGE ( 'NONE', *, *, #121256, .F. ) ;
#65379=EDGE_CURVE ( 'NONE', #143546, #3467, #19436, .T. ) ;
#65383=DIRECTION ( 'NONE',  ( 0.3543493200069162685, -0.000000000000000000, -0.9351131265310288487 ) ) ;
#65384=CARTESIAN_POINT ( 'NONE',  ( -20.99999999999984723, -6.033600742197678279, 5.000000000000000000 ) ) ;
#65385=FACE_BOUND ( 'NONE', #46581, .T. ) ;
#65387=DIRECTION ( 'NONE',  ( -0.7071067811865486830, -0.7071067811865464625, 0.000000000000000000 ) ) ;
#65388=EDGE_CURVE ( 'NONE', #87654, #9178, #96952, .T. ) ;
#65390=DIRECTION ( 'NONE',  ( 0.7071067811865487940, 0.7071067811865463515, 0.000000000000000000 ) ) ;
#65392=CARTESIAN_POINT ( 'NONE',  ( 20.18753812416037974, -22.22500000000000142, 4.000000000000000000 ) ) ;
#65393=ORIENTED_EDGE ( 'NONE', *, *, #22680, .T. ) ;
#65396=ORIENTED_EDGE ( 'NONE', *, *, #133515, .T. ) ;
#65398=ORIENTED_EDGE ( 'NONE', *, *, #33594, .F. ) ;
#65399=FACE_OUTER_BOUND ( 'NONE', #79740, .T. ) ;
#65402=EDGE_LOOP ( 'NONE', ( #112806, #5652, #139182, #54243 ) ) ;
#65403=CARTESIAN_POINT ( 'NONE',  ( 34.75611968250419892, -4.294349301475905101, 4.955485411084876723 ) ) ;
#65405=DIRECTION ( 'NONE',  ( 0.7071067811865486830, -0.7071067811865464625, -0.000000000000000000 ) ) ;
#65407=ADVANCED_FACE ( 'NONE', ( #18697 ), #141202, .F. ) ;
#65409=VECTOR ( 'NONE', #13482, 1000.000000000000000 ) ;
#65410=LINE ( 'NONE', #142935, #142041 ) ;
#65411=FACE_OUTER_BOUND ( 'NONE', #33654, .T. ) ;
#65412=VERTEX_POINT ( 'NONE', #73822 ) ;
#65413=ORIENTED_EDGE ( 'NONE', *, *, #53739, .T. ) ;
#65414=ORIENTED_EDGE ( 'NONE', *, *, #140438, .F. ) ;
#65416=DIRECTION ( 'NONE',  ( 0.7071067811865487940, -0.7071067811865463515, 0.000000000000000000 ) ) ;
#65417=FACE_OUTER_BOUND ( 'NONE', #88326, .T. ) ;
#65418=ORIENTED_EDGE ( 'NONE', *, *, #16223, .T. ) ;
#65419=VERTEX_POINT ( 'NONE', #130360 ) ;
#65421=LINE ( 'NONE', #108857, #119700 ) ;
#65422=ADVANCED_FACE ( 'NONE', ( #117994 ), #95563, .F. ) ;
#65423=ADVANCED_FACE ( 'NONE', ( #9982 ), #54250, .F. ) ;
#65424=CARTESIAN_POINT ( 'NONE',  ( 15.32816939922342847, -3.740707523384238176, 4.000000000000000000 ) ) ;
#65425=ORIENTED_EDGE ( 'NONE', *, *, #42528, .F. ) ;
#65427=CARTESIAN_POINT ( 'NONE',  ( -3.838293875473783423, -6.740707523384212863, 16.75550250614866599 ) ) ;
#65429=LINE ( 'NONE', #42953, #78561 ) ;
#65430=ORIENTED_EDGE ( 'NONE', *, *, #97066, .T. ) ;
#65432=( BOUNDED_CURVE ( )  B_SPLINE_CURVE ( 3, ( #111662, #55874, #135565, #1433 ),
 .UNSPECIFIED., .F., .T. ) 
 B_SPLINE_CURVE_WITH_KNOTS ( ( 4, 4 ),
 ( 5.920967161967927161, 7.341195215986585865 ),
 .UNSPECIFIED. ) 
 CURVE ( )  GEOMETRIC_REPRESENTATION_ITEM ( )  RATIONAL_B_SPLINE_CURVE ( ( 1.000000000000000000, 0.8388583629366725969, 0.8388583629366725969, 1.000000000000000000 ) ) 
 REPRESENTATION_ITEM ( '' )  );
#65433=EDGE_CURVE ( 'NONE', #111218, #79059, #86132, .T. ) ;
#65434=LINE ( 'NONE', #92, #14115 ) ;
#65435=VECTOR ( 'NONE', #33793, 1000.000000000000000 ) ;
#65436=CARTESIAN_POINT ( 'NONE',  ( 18.18398860626898994, 28.73617430169800002, 5.000000000000000000 ) ) ;
#65437=LINE ( 'NONE', #141545, #102740 ) ;
#65439=DIRECTION ( 'NONE',  ( 0.7071067811865486830, -0.7071067811865464625, -0.000000000000000000 ) ) ;
#65440=AXIS2_PLACEMENT_3D ( 'NONE', #26591, #81717, #82410 ) ;
#65442=DIRECTION ( 'NONE',  ( 0.7071067811865486830, -0.7071067811865464625, -0.000000000000000000 ) ) ;
#65443=DIRECTION ( 'NONE',  ( -0.3543493200069162685, -0.000000000000000000, -0.9351131265310288487 ) ) ;
#65444=DIRECTION ( 'NONE',  ( -0.7071067811865486830, 0.7071067811865464625, 0.000000000000000000 ) ) ;
#65446=ORIENTED_EDGE ( 'NONE', *, *, #107199, .F. ) ;
#65447=CARTESIAN_POINT ( 'NONE',  ( 77.99451991528749772, 28.92564299267992567, 4.000000000000000000 ) ) ;
#65448=CARTESIAN_POINT ( 'NONE',  ( 0.2997448713915885632, -27.71228299555206220, 4.000000000000000000 ) ) ;
#65449=EDGE_LOOP ( 'NONE', ( #141520, #45862, #106020, #107986 ) ) ;
#65450=ADVANCED_FACE ( 'NONE', ( #119436 ), #74554, .F. ) ;
#65451=VECTOR ( 'NONE', #85103, 1000.000000000000000 ) ;
#65453=DIRECTION ( 'NONE',  ( -0.000000000000000000, 0.3543493200069153248, 0.9351131265310292928 ) ) ;
#65454=VERTEX_POINT ( 'NONE', #30315 ) ;
#65455=CARTESIAN_POINT ( 'NONE',  ( 0.000000000000000000, 0.000000000000000000, 5.000000000000000000 ) ) ;
#65456=ORIENTED_EDGE ( 'NONE', *, *, #106284, .T. ) ;
#65457=EDGE_LOOP ( 'NONE', ( #141082, #10356, #12865, #97638, #25694 ) ) ;
#65458=VECTOR ( 'NONE', #103606, 1000.000000000000227 ) ;
#65460=CARTESIAN_POINT ( 'NONE',  ( 29.99999999999979394, -3.485240976185050243, -4.108735105802328036 ) ) ;
#65461=( BOUNDED_CURVE ( )  B_SPLINE_CURVE ( 3, ( #77209, #31538, #98224, #61516 ),
 .UNSPECIFIED., .F., .F. ) 
 B_SPLINE_CURVE_WITH_KNOTS ( ( 4, 4 ),
 ( 5.920967161967927161, 7.341195215986588529 ),
 .UNSPECIFIED. ) 
 CURVE ( )  GEOMETRIC_REPRESENTATION_ITEM ( )  RATIONAL_B_SPLINE_CURVE ( ( 1.000000000000000000, 0.8388583629366720418, 0.8388583629366720418, 1.000000000000000000 ) ) 
 REPRESENTATION_ITEM ( '' )  );
#65462=VERTEX_POINT ( 'NONE', #108545 ) ;
#65463=LINE ( 'NONE', #21917, #45973 ) ;
#65464=DIRECTION ( 'NONE',  ( -0.7071067811865486830, 0.7071067811865464625, 0.000000000000000000 ) ) ;
#65465=CARTESIAN_POINT ( 'NONE',  ( 7.499999999999948486, 15.43112307739203182, 4.000000000000000000 ) ) ;
#65466=ORIENTED_EDGE ( 'NONE', *, *, #88190, .F. ) ;
#65467=ADVANCED_FACE ( 'NONE', ( #35347 ), #54939, .F. ) ;
#65469=LINE ( 'NONE', #19779, #95305 ) ;
#65470=LINE ( 'NONE', #54580, #91054 ) ;
#65471=VECTOR ( 'NONE', #79192, 1000.000000000000000 ) ;
#65474=CARTESIAN_POINT ( 'NONE',  ( 0.1839886062690032631, 28.73617430169787568, 5.000000000000000000 ) ) ;
#65475=ADVANCED_FACE ( 'NONE', ( #44059 ), #25132, .F. ) ;
#65476=VECTOR ( 'NONE', #107479, 1000.000000000000227 ) ;
#65477=EDGE_CURVE ( 'NONE', #47195, #22650, #33216, .T. ) ;
#65478=AXIS2_PLACEMENT_3D ( 'NONE', #61156, #105304, #5960 ) ;
#65480=EDGE_LOOP ( 'NONE', ( #91143, #17442, #111815, #403 ) ) ;
#65481=VERTEX_POINT ( 'NONE', #88280 ) ;
#65482=ORIENTED_EDGE ( 'NONE', *, *, #141493, .F. ) ;
#65484=VECTOR ( 'NONE', #106266, 1000.000000000000227 ) ;
#65485=DIRECTION ( 'NONE',  ( 0.3543493200069162685, -0.000000000000000000, -0.9351131265310288487 ) ) ;
#65487=PLANE ( 'NONE',  #122700 ) ;
#65488=EDGE_CURVE ( 'NONE', #118275, #35117, #78838, .T. ) ;
#65489=VERTEX_POINT ( 'NONE', #99110 ) ;
#65490=FACE_OUTER_BOUND ( 'NONE', #142355, .T. ) ;
#65491=CARTESIAN_POINT ( 'NONE',  ( 2.816011393730999401, 28.73617430169785436, 5.000000000000000000 ) ) ;
#65492=EDGE_CURVE ( 'NONE', #36317, #53631, #80273, .T. ) ;
#65494=LINE ( 'NONE', #51021, #33822 ) ;
#65497=LINE ( 'NONE', #98095, #27922 ) ;
#65498=DIRECTION ( 'NONE',  ( -0.7071067811865486830, -0.7071067811865464625, -0.000000000000000000 ) ) ;
#65499=DIRECTION ( 'NONE',  ( -0.7071067811865486830, -0.7071067811865464625, 0.000000000000000000 ) ) ;
#65501=LINE ( 'NONE', #23371, #12674 ) ;
#65505=( BOUNDED_CURVE ( )  B_SPLINE_CURVE ( 3, ( #50923, #48785, #92990, #136483 ),
 .UNSPECIFIED., .F., .T. ) 
 B_SPLINE_CURVE_WITH_KNOTS ( ( 4, 4 ),
 ( 4.350170835173029715, 4.500739107949259576 ),
 .UNSPECIFIED. ) 
 CURVE ( )  GEOMETRIC_REPRESENTATION_ITEM ( )  RATIONAL_B_SPLINE_CURVE ( ( 1.000000000000000000, 0.9981116584018945304, 0.9981116584018945304, 1.000000000000000000 ) ) 
 REPRESENTATION_ITEM ( '' )  );
#65506=DIRECTION ( 'NONE',  ( -0.3543493200069162685, -0.000000000000000000, -0.9351131265310288487 ) ) ;
#65507=EDGE_CURVE ( 'NONE', #38910, #18696, #132529, .T. ) ;
#65508=AXIS2_PLACEMENT_3D ( 'NONE', #104650, #61217, #14793 ) ;
#65509=CARTESIAN_POINT ( 'NONE',  ( 36.18398860626899705, 28.73617430169812437, 5.000000000000000000 ) ) ;
#65510=ORIENTED_EDGE ( 'NONE', *, *, #1464, .T. ) ;
#65511=ORIENTED_EDGE ( 'NONE', *, *, #30459, .F. ) ;
#65513=EDGE_CURVE ( 'NONE', #13150, #119701, #46223, .T. ) ;
#65514=LINE ( 'NONE', #119131, #67074 ) ;
#65515=DIRECTION ( 'NONE',  ( -0.6830127018922181881, 0.6830127018922202975, -0.2588190451025214056 ) ) ;
#65516=VERTEX_POINT ( 'NONE', #110005 ) ;
#65517=EDGE_CURVE ( 'NONE', #123774, #118884, #112862, .T. ) ;
#65518=PLANE ( 'NONE',  #105706 ) ;
#65519=AXIS2_PLACEMENT_3D ( 'NONE', #59355, #135477, #102126 ) ;
#65520=DIRECTION ( 'NONE',  ( 1.000000000000000000, 0.000000000000000000, 0.000000000000000000 ) ) ;
#65522=VECTOR ( 'NONE', #49748, 1000.000000000000000 ) ;
#65525=ORIENTED_EDGE ( 'NONE', *, *, #116602, .T. ) ;
#65526=EDGE_LOOP ( 'NONE', ( #63288, #133285, #24226, #104301 ) ) ;
#65527=EDGE_CURVE ( 'NONE', #59092, #24092, #22260, .T. ) ;
#65528=VECTOR ( 'NONE', #57853, 1000.000000000000000 ) ;
#65529=PLANE ( 'NONE',  #137215 ) ;
#65530=CARTESIAN_POINT ( 'NONE',  ( 18.53421140649331633, 9.121673282332597665, 4.000000000000000000 ) ) ;
#65531=CARTESIAN_POINT ( 'NONE',  ( 42.48921356237308800, -27.52281430457085065, 5.000000000000000000 ) ) ;
#65532=CARTESIAN_POINT ( 'NONE',  ( 0.000000000000000000, 0.000000000000000000, 5.000000000000000000 ) ) ;
#65534=DIRECTION ( 'NONE',  ( -0.000000000000000000, 0.000000000000000000, 1.000000000000000000 ) ) ;
#65535=LINE ( 'NONE', #121293, #106649 ) ;
#65536=CARTESIAN_POINT ( 'NONE',  ( 0.000000000000000000, 0.000000000000000000, 5.000000000000000000 ) ) ;
#65537=VERTEX_POINT ( 'NONE', #110694 ) ;
#65539=DIRECTION ( 'NONE',  ( 0.7071067811865486830, -0.7071067811865464625, -0.000000000000000000 ) ) ;
#65540=FACE_OUTER_BOUND ( 'NONE', #85053, .T. ) ;
#65541=LINE ( 'NONE', #19836, #79661 ) ;
#65542=EDGE_CURVE ( 'NONE', #70976, #97364, #124463, .T. ) ;
#65544=CARTESIAN_POINT ( 'NONE',  ( 10.49999999999993250, -4.796895815301006394, -3.611700055028658429 ) ) ;
#65546=EDGE_CURVE ( 'NONE', #108369, #108304, #122296, .T. ) ;
#65547=ORIENTED_EDGE ( 'NONE', *, *, #82626, .F. ) ;
#65552=CARTESIAN_POINT ( 'NONE',  ( -4.580140136459718292, -22.22500000000000142, 16.49880175272448568 ) ) ;
#65553=PLANE ( 'NONE',  #24688 ) ;
#65555=ORIENTED_EDGE ( 'NONE', *, *, #124037, .F. ) ;
#65556=CARTESIAN_POINT ( 'NONE',  ( 48.48921356237309510, -27.52281430457089328, 5.000000000000000000 ) ) ;
#65557=DIRECTION ( 'NONE',  ( -0.000000000000000000, -0.3543493200069152693, 0.9351131265310292928 ) ) ;
#65559=VERTEX_POINT ( 'NONE', #55654 ) ;
#65561=CARTESIAN_POINT ( 'NONE',  ( -39.48921356237310221, -27.52281430457082934, 5.000000000000000000 ) ) ;
#65562=ORIENTED_EDGE ( 'NONE', *, *, #50992, .T. ) ;
#65563=DIRECTION ( 'NONE',  ( 0.7071067811865487940, -0.7071067811865463515, 0.000000000000000000 ) ) ;
#65564=CARTESIAN_POINT ( 'NONE',  ( -20.67183060077633527, -9.740707523384180888, 4.000000000000000000 ) ) ;
#65565=CARTESIAN_POINT ( 'NONE',  ( 42.18398860626899705, 28.73617430169816700, 5.000000000000000000 ) ) ;
#65566=AXIS2_PLACEMENT_3D ( 'NONE', #134538, #36619, #2545 ) ;
#65567=DIRECTION ( 'NONE',  ( 0.6830127018922180770, -0.6830127018922204085, -0.2588190451025213501 ) ) ;
#65568=FACE_BOUND ( 'NONE', #142186, .T. ) ;
#65569=CARTESIAN_POINT ( 'NONE',  ( -25.49999999999982592, -8.568876922607724822, 4.000000000000000000 ) ) ;
#65572=CARTESIAN_POINT ( 'NONE',  ( 0.000000000000000000, 0.000000000000000000, 5.000000000000000000 ) ) ;
#65574=ORIENTED_EDGE ( 'NONE', *, *, #2027, .F. ) ;
#65575=CARTESIAN_POINT ( 'NONE',  ( 35.99451991528749772, 28.92564299267963079, 4.000000000000000000 ) ) ;
#65577=VERTEX_POINT ( 'NONE', #33901 ) ;
#65578=ORIENTED_EDGE ( 'NONE', *, *, #6028, .F. ) ;
#65580=ORIENTED_EDGE ( 'NONE', *, *, #69041, .F. ) ;
#65581=PLANE ( 'NONE',  #1307 ) ;
#65582=CARTESIAN_POINT ( 'NONE',  ( 34.42499999999998295, 22.22500000000000142, 5.000000000000000000 ) ) ;
#65583=EDGE_CURVE ( 'NONE', #19566, #47325, #22969, .T. ) ;
#65584=ORIENTED_EDGE ( 'NONE', *, *, #7092, .F. ) ;
#65585=LINE ( 'NONE', #101012, #123160 ) ;
#65586=VECTOR ( 'NONE', #129784, 1000.000000000000227 ) ;
#65587=AXIS2_PLACEMENT_3D ( 'NONE', #63961, #74859, #107442 ) ;
#65589=PLANE ( 'NONE',  #71580 ) ;
#65591=LINE ( 'NONE', #64845, #113030 ) ;
#65592=DIRECTION ( 'NONE',  ( -0.6830127018922180770, -0.6830127018922204085, -0.2588190451025213501 ) ) ;
#65593=CARTESIAN_POINT ( 'NONE',  ( -24.78162688292477256, 21.74787736706806385, 4.999607392498049308 ) ) ;
#65594=FACE_OUTER_BOUND ( 'NONE', #131932, .T. ) ;
#65595=ORIENTED_EDGE ( 'NONE', *, *, #58628, .F. ) ;
#65596=AXIS2_PLACEMENT_3D ( 'NONE', #27691, #50185, #105947 ) ;
#65598=DIRECTION ( 'NONE',  ( -0.7071067811865486830, -0.7071067811865464625, 0.000000000000000000 ) ) ;
#65599=ORIENTED_EDGE ( 'NONE', *, *, #97649, .T. ) ;
#65600=DIRECTION ( 'NONE',  ( -0.6830127018922181881, 0.6830127018922202975, -0.2588190451025214056 ) ) ;
#65602=EDGE_CURVE ( 'NONE', #71954, #80946, #12118, .T. ) ;
#65603=ORIENTED_EDGE ( 'NONE', *, *, #67377, .T. ) ;
#65604=ORIENTED_EDGE ( 'NONE', *, *, #112311, .T. ) ;
#65605=ADVANCED_FACE ( 'NONE', ( #90404 ), #34605, .F. ) ;
#65607=EDGE_LOOP ( 'NONE', ( #19485, #52501, #126822, #74045 ) ) ;
#65608=CARTESIAN_POINT ( 'NONE',  ( 12.18398860626900060, 28.73617430169795739, 5.000000000000000000 ) ) ;
#65609=EDGE_CURVE ( 'NONE', #80548, #37747, #135369, .T. ) ;
#65611=DIRECTION ( 'NONE',  ( -0.7071067811865487940, 0.7071067811865463515, 0.000000000000000000 ) ) ;
#65616=EDGE_CURVE ( 'NONE', #37037, #132203, #14270, .T. ) ;
#65618=ORIENTED_EDGE ( 'NONE', *, *, #14210, .F. ) ;
#65619=DIRECTION ( 'NONE',  ( 0.7071067811865486830, -0.7071067811865464625, -0.000000000000000000 ) ) ;
#65620=DIRECTION ( 'NONE',  ( 0.6830127018922181881, 0.6830127018922202975, -0.2588190451025214056 ) ) ;
#65621=DIRECTION ( 'NONE',  ( -0.000000000000000000, -0.3543493200069152693, 0.9351131265310292928 ) ) ;
#65622=VERTEX_POINT ( 'NONE', #138927 ) ;
#65623=ORIENTED_EDGE ( 'NONE', *, *, #26560, .T. ) ;
#65625=DIRECTION ( 'NONE',  ( -0.7071067811865486830, -0.7071067811865464625, -0.000000000000000000 ) ) ;
#65626=AXIS2_PLACEMENT_3D ( 'NONE', #98897, #77198, #8298 ) ;
#65627=CARTESIAN_POINT ( 'NONE',  ( -25.00193056682080339, -22.22500000000000142, 4.500000000000000888 ) ) ;
#65629=ORIENTED_EDGE ( 'NONE', *, *, #141796, .F. ) ;
#65630=FACE_OUTER_BOUND ( 'NONE', #95734, .T. ) ;
#65631=ORIENTED_EDGE ( 'NONE', *, *, #15759, .F. ) ;
#65633=ORIENTED_EDGE ( 'NONE', *, *, #92572, .F. ) ;
#65636=EDGE_CURVE ( 'NONE', #93893, #55894, #25862, .T. ) ;
#65637=CARTESIAN_POINT ( 'NONE',  ( 48.48921356237309510, -27.52281430457089328, 5.000000000000000000 ) ) ;
#65638=DIRECTION ( 'NONE',  ( -0.7071067811865486830, -0.7071067811865464625, -0.000000000000000000 ) ) ;
#65639=LINE ( 'NONE', #132310, #63090 ) ;
#65641=DIRECTION ( 'NONE',  ( -0.7071067811865487940, 0.7071067811865463515, -0.000000000000000000 ) ) ;
#65642=LINE ( 'NONE', #118535, #6592 ) ;
#65643=ORIENTED_EDGE ( 'NONE', *, *, #112928, .T. ) ;
#65644=CARTESIAN_POINT ( 'NONE',  ( -8.700255128608413102, -27.71228299555199825, 4.000000000000000000 ) ) ;
#65645=VERTEX_POINT ( 'NONE', #128061 ) ;
#65646=EDGE_CURVE ( 'NONE', #54301, #58586, #105546, .T. ) ;
#65647=EDGE_CURVE ( 'NONE', #52699, #116759, #48334, .T. ) ;
#65648=CARTESIAN_POINT ( 'NONE',  ( -27.33010218547248726, 17.25929247661553845, 19.83885114516077408 ) ) ;
#65649=AXIS2_PLACEMENT_3D ( 'NONE', #96018, #76436, #18428 ) ;
#65651=PLANE ( 'NONE',  #140816 ) ;
#65652=AXIS2_PLACEMENT_3D ( 'NONE', #78795, #14935, #56365 ) ;
#65653=ORIENTED_EDGE ( 'NONE', *, *, #143517, .F. ) ;
#65654=FACE_OUTER_BOUND ( 'NONE', #41434, .T. ) ;
#65655=CARTESIAN_POINT ( 'NONE',  ( 0.000000000000000000, 0.000000000000000000, 5.000000000000000000 ) ) ;
#65656=LINE ( 'NONE', #90951, #69940 ) ;
#65658=ORIENTED_EDGE ( 'NONE', *, *, #17629, .T. ) ;
#65659=ADVANCED_FACE ( 'NONE', ( #114296 ), #16385, .T. ) ;
#65664=CARTESIAN_POINT ( 'NONE',  ( 34.92499999999998295, 9.662461875838909364, 4.000000000000000000 ) ) ;
#65665=CARTESIAN_POINT ( 'NONE',  ( -34.49999999999974420, -20.94567065516883275, 4.994342998332162331 ) ) ;
#65668=EDGE_CURVE ( 'NONE', #110890, #136749, #58556, .T. ) ;
#65669=EDGE_CURVE ( 'NONE', #31974, #10130, #93262, .T. ) ;
#65670=CARTESIAN_POINT ( 'NONE',  ( -19.49999999999986500, 14.14708470758589165, -0.5283514160166116191 ) ) ;
#65671=CARTESIAN_POINT ( 'NONE',  ( -14.57672154193637937, 11.25929247661560240, 17.85071094206588072 ) ) ;
#65672=VERTEX_POINT ( 'NONE', #60686 ) ;
#65673=CARTESIAN_POINT ( 'NONE',  ( -21.48921356237309155, -27.52281430457070499, 5.000000000000000000 ) ) ;
#65674=EDGE_LOOP ( 'NONE', ( #124756, #75527, #76911, #389 ) ) ;
#65676=DIRECTION ( 'NONE',  ( -0.7071067811865487940, 0.7071067811865463515, -0.000000000000000000 ) ) ;
#65680=DIRECTION ( 'NONE',  ( 0.7071067811865487940, -0.7071067811865463515, 0.000000000000000000 ) ) ;
#65682=ADVANCED_FACE ( 'NONE', ( #28742 ), #64219, .F. ) ;
#65684=LINE ( 'NONE', #117833, #119456 ) ;
#65685=ORIENTED_EDGE ( 'NONE', *, *, #36206, .T. ) ;
#65688=CARTESIAN_POINT ( 'NONE',  ( -30.48921356237309510, -27.52281430457076894, 5.000000000000000000 ) ) ;
#65689=DIRECTION ( 'NONE',  ( -0.7071067811865486830, -0.7071067811865464625, 0.000000000000000000 ) ) ;
#65690=CARTESIAN_POINT ( 'NONE',  ( 14.51078643762690490, -27.52281430457045275, 5.000000000000000000 ) ) ;
#65692=DIRECTION ( 'NONE',  ( -0.7071067811865486830, -0.7071067811865464625, -0.000000000000000000 ) ) ;
#65693=VECTOR ( 'NONE', #110637, 1000.000000000000000 ) ;
#65694=DIRECTION ( 'NONE',  ( -0.3543493200069162685, -0.000000000000000000, -0.9351131265310288487 ) ) ;
#65695=VERTEX_POINT ( 'NONE', #9818 ) ;
#65697=EDGE_CURVE ( 'NONE', #137044, #69532, #95400, .T. ) ;
#65700=DIRECTION ( 'NONE',  ( -0.6830127018922181881, 0.6830127018922202975, -0.2588190451025214056 ) ) ;
#65701=ORIENTED_EDGE ( 'NONE', *, *, #60367, .F. ) ;
#65702=EDGE_CURVE ( 'NONE', #71830, #48713, #52609, .T. ) ;
#65703=AXIS2_PLACEMENT_3D ( 'NONE', #88405, #45627, #110814 ) ;
#65704=LINE ( 'NONE', #53333, #106938 ) ;
#65705=ORIENTED_EDGE ( 'NONE', *, *, #102626, .F. ) ;
#65707=LINE ( 'NONE', #13925, #68655 ) ;
#65708=DIRECTION ( 'NONE',  ( 0.7071067811865487940, 0.7071067811865463515, 0.000000000000000000 ) ) ;
#65709=ORIENTED_EDGE ( 'NONE', *, *, #113123, .T. ) ;
#65710=DIRECTION ( 'NONE',  ( -0.7071067811865487940, 0.7071067811865463515, 0.000000000000000000 ) ) ;
#65711=LINE ( 'NONE', #54801, #40665 ) ;
#65712=CARTESIAN_POINT ( 'NONE',  ( -0.8124618758394642759, -22.22500000000000142, 4.000000000000000000 ) ) ;
#65714=LINE ( 'NONE', #9087, #32390 ) ;
#65715=DIRECTION ( 'NONE',  ( -0.000000000000000000, 0.000000000000000000, 1.000000000000000000 ) ) ;
#65716=VERTEX_POINT ( 'NONE', #72984 ) ;
#65717=LINE ( 'NONE', #119312, #9043 ) ;
#65719=DIRECTION ( 'NONE',  ( 1.000000000000000000, 0.000000000000000000, 0.000000000000000000 ) ) ;
#65722=ORIENTED_EDGE ( 'NONE', *, *, #1137, .T. ) ;
#65723=EDGE_CURVE ( 'NONE', #48454, #116545, #19972, .T. ) ;
#65726=VECTOR ( 'NONE', #89860, 1000.000000000000000 ) ;
#65728=CARTESIAN_POINT ( 'NONE',  ( -11.20710678118646975, 12.75929247661559174, 5.000000000000000000 ) ) ;
#65734=CARTESIAN_POINT ( 'NONE',  ( -24.32997752056147078, -22.22500000000000142, 0.9851499198022823922 ) ) ;
#65736=VECTOR ( 'NONE', #72037, 1000.000000000000000 ) ;
#65737=EDGE_LOOP ( 'NONE', ( #40397, #76809, #64590, #90327 ) ) ;
#65739=LINE ( 'NONE', #97586, #88369 ) ;
#65740=DIRECTION ( 'NONE',  ( -0.000000000000000000, 0.000000000000000000, 1.000000000000000000 ) ) ;
#65741=CARTESIAN_POINT ( 'NONE',  ( -7.998069433178966570, -22.22500000000000142, 4.500000000000000888 ) ) ;
#65742=( BOUNDED_CURVE ( )  B_SPLINE_CURVE ( 3, ( #129198, #63970, #19026, #86444 ),
 .UNSPECIFIED., .F., .T. ) 
 B_SPLINE_CURVE_WITH_KNOTS ( ( 4, 4 ),
 ( 5.106027341939291198, 6.645403452391242638 ),
 .UNSPECIFIED. ) 
 CURVE ( )  GEOMETRIC_REPRESENTATION_ITEM ( )  RATIONAL_B_SPLINE_CURVE ( ( 1.000000000000000000, 0.8120851936182310604, 0.8120851936182310604, 1.000000000000000000 ) ) 
 REPRESENTATION_ITEM ( '' )  );
#65743=ORIENTED_EDGE ( 'NONE', *, *, #7751, .T. ) ;
#65745=DIRECTION ( 'NONE',  ( 0.6830127018922181881, 0.6830127018922202975, -0.2588190451025214056 ) ) ;
#65746=DIRECTION ( 'NONE',  ( -0.7071067811865487940, 0.7071067811865463515, 0.000000000000000000 ) ) ;
#65747=PLANE ( 'NONE',  #16584 ) ;
#65748=LINE ( 'NONE', #141098, #71478 ) ;
#65750=VECTOR ( 'NONE', #89106, 1000.000000000000000 ) ;
#65751=CARTESIAN_POINT ( 'NONE',  ( -20.28242261357419451, -21.73023691814494285, 5.000000000000000888 ) ) ;
#65752=ORIENTED_EDGE ( 'NONE', *, *, #62336, .F. ) ;
#65754=ORIENTED_EDGE ( 'NONE', *, *, #62707, .F. ) ;
#65756=ORIENTED_EDGE ( 'NONE', *, *, #27824, .T. ) ;
#65757=ORIENTED_EDGE ( 'NONE', *, *, #140438, .T. ) ;
#65758=VECTOR ( 'NONE', #49061, 1000.000000000000227 ) ;
#65760=CARTESIAN_POINT ( 'NONE',  ( -1.828169399223519953, -11.24070752338416845, 4.000000000000000000 ) ) ;
#65761=DIRECTION ( 'NONE',  ( -0.7071067811865486830, -0.7071067811865464625, -0.000000000000000000 ) ) ;
#65762=ORIENTED_EDGE ( 'NONE', *, *, #95210, .F. ) ;
#65765=LINE ( 'NONE', #33824, #138364 ) ;
#65766=CARTESIAN_POINT ( 'NONE',  ( -20.88987624306225399, 8.854559187742358617, 4.414246686754470517 ) ) ;
#65767=EDGE_CURVE ( 'NONE', #61191, #93479, #108378, .T. ) ;
#65768=LINE ( 'NONE', #109932, #92447 ) ;
#65769=EDGE_CURVE ( 'NONE', #18049, #132699, #30889, .T. ) ;
#65770=VECTOR ( 'NONE', #53264, 999.9999999999998863 ) ;
#65771=PLANE ( 'NONE',  #79185 ) ;
#65772=VERTEX_POINT ( 'NONE', #117837 ) ;
#65773=DIRECTION ( 'NONE',  ( -0.6830127018922181881, 0.6830127018922202975, -0.2588190451025214056 ) ) ;
#65774=DIRECTION ( 'NONE',  ( -0.6830127018922181881, 0.6830127018922202975, -0.2588190451025214056 ) ) ;
#65775=EDGE_CURVE ( 'NONE', #108829, #566, #62806, .T. ) ;
#65776=EDGE_CURVE ( 'NONE', #41224, #100224, #117139, .T. ) ;
#65778=VERTEX_POINT ( 'NONE', #9057 ) ;
#65779=EDGE_CURVE ( 'NONE', #53886, #70033, #128744, .T. ) ;
#65780=EDGE_CURVE ( 'NONE', #93689, #129451, #31589, .T. ) ;
#65781=ORIENTED_EDGE ( 'NONE', *, *, #59259, .F. ) ;
#65783=ORIENTED_EDGE ( 'NONE', *, *, #108426, .F. ) ;
#65784=EDGE_CURVE ( 'NONE', #133821, #47983, #75812, .T. ) ;
#65786=FACE_OUTER_BOUND ( 'NONE', #101862, .T. ) ;
#65787=VECTOR ( 'NONE', #112989, 999.9999999999998863 ) ;
#65790=LINE ( 'NONE', #20069, #139758 ) ;
#65792=VERTEX_POINT ( 'NONE', #42489 ) ;
#65793=CARTESIAN_POINT ( 'NONE',  ( 2.816011393730999401, 28.73617430169785436, 5.000000000000000000 ) ) ;
#65794=CARTESIAN_POINT ( 'NONE',  ( -0.1839886062690032631, 28.73617430169787568, 5.000000000000000000 ) ) ;
#65795=AXIS2_PLACEMENT_3D ( 'NONE', #136495, #34516, #78041 ) ;
#65797=CARTESIAN_POINT ( 'NONE',  ( -14.99999999999990230, 10.21212019023807649, -2.019456568337765212 ) ) ;
#65798=EDGE_CURVE ( 'NONE', #68468, #122052, #51921, .T. ) ;
#65799=EDGE_LOOP ( 'NONE', ( #79104, #6526, #30468, #33319 ) ) ;
#65800=CARTESIAN_POINT ( 'NONE',  ( 22.42819999999999681, 3.174999999999997158, 5.000000000000000000 ) ) ;
#65801=ORIENTED_EDGE ( 'NONE', *, *, #124735, .F. ) ;
#65802=EDGE_LOOP ( 'NONE', ( #109170, #137622, #5514, #5456 ) ) ;
#65803=ORIENTED_EDGE ( 'NONE', *, *, #136436, .F. ) ;
#65805=ORIENTED_EDGE ( 'NONE', *, *, #141309, .T. ) ;
#65806=PLANE ( 'NONE',  #81658 ) ;
#65807=DIRECTION ( 'NONE',  ( -0.7071067811865486830, -0.7071067811865464625, 0.000000000000000000 ) ) ;
#65809=DIRECTION ( 'NONE',  ( -0.7071067811865487940, 0.7071067811865463515, 0.000000000000000000 ) ) ;
#65810=ORIENTED_EDGE ( 'NONE', *, *, #125818, .T. ) ;
#65811=VECTOR ( 'NONE', #51999, 1000.000000000000227 ) ;
#65812=ADVANCED_FACE ( 'NONE', ( #63532 ), #130918, .F. ) ;
#65813=VECTOR ( 'NONE', #100595, 1000.000000000000000 ) ;
#65815=LINE ( 'NONE', #109974, #11500 ) ;
#65818=ORIENTED_EDGE ( 'NONE', *, *, #34314, .T. ) ;
#65819=ORIENTED_EDGE ( 'NONE', *, *, #134052, .T. ) ;
#65820=EDGE_CURVE ( 'NONE', #20392, #103852, #141040, .T. ) ;
#65823=DIRECTION ( 'NONE',  ( 0.7071067811865487940, -0.7071067811865463515, 0.000000000000000000 ) ) ;
#65824=FACE_OUTER_BOUND ( 'NONE', #9492, .T. ) ;
#65825=DIRECTION ( 'NONE',  ( 0.7071067811865487940, -0.7071067811865463515, 0.000000000000000000 ) ) ;
#65826=EDGE_CURVE ( 'NONE', #89630, #30859, #75115, .T. ) ;
#65827=DIRECTION ( 'NONE',  ( 0.7071067811865486830, -0.7071067811865464625, -0.000000000000000000 ) ) ;
#65828=AXIS2_PLACEMENT_3D ( 'NONE', #136914, #80421, #14427 ) ;
#65830=PLANE ( 'NONE',  #122769 ) ;
#65831=LINE ( 'NONE', #32451, #60478 ) ;
#65834=FACE_OUTER_BOUND ( 'NONE', #708, .T. ) ;
#65835=ORIENTED_EDGE ( 'NONE', *, *, #5937, .T. ) ;
#65838=VECTOR ( 'NONE', #133549, 1000.000000000000000 ) ;
#65839=ADVANCED_FACE ( 'NONE', ( #123618 ), #88837, .F. ) ;
#65840=DIRECTION ( 'NONE',  ( 1.000000000000000000, 0.000000000000000000, 0.000000000000000000 ) ) ;
#65841=DIRECTION ( 'NONE',  ( -0.6830127018922181881, 0.6830127018922202975, -0.2588190451025214056 ) ) ;
#65842=VERTEX_POINT ( 'NONE', #110537 ) ;
#65843=VECTOR ( 'NONE', #51687, 1000.000000000000227 ) ;
#65845=ORIENTED_EDGE ( 'NONE', *, *, #72917, .T. ) ;
#65847=ORIENTED_EDGE ( 'NONE', *, *, #11562, .T. ) ;
#65848=CARTESIAN_POINT ( 'NONE',  ( -29.20003122016818509, 8.259292476615634371, 16.85664084051848022 ) ) ;
#65851=AXIS2_PLACEMENT_3D ( 'NONE', #74497, #83955, #128843 ) ;
#65852=CARTESIAN_POINT ( 'NONE',  ( -8.999999999999932498, -10.44781430457072169, 5.000000000000000000 ) ) ;
#65854=CARTESIAN_POINT ( 'NONE',  ( -23.99999999999984013, -2.904428200921339354, -6.989807076074889380 ) ) ;
#65856=LINE ( 'NONE', #119443, #138885 ) ;
#65857=ADVANCED_FACE ( 'NONE', ( #43895 ), #44646, .F. ) ;
#65858=CARTESIAN_POINT ( 'NONE',  ( -11.99999999999992006, -4.068876922607777225, 4.000000000000000000 ) ) ;
#65859=DIRECTION ( 'NONE',  ( -0.000000000000000000, -0.3543493200069152693, 0.9351131265310292928 ) ) ;
#65862=DIRECTION ( 'NONE',  ( 0.6830127018922181881, 0.6830127018922202975, -0.2588190451025214056 ) ) ;
#65863=FACE_OUTER_BOUND ( 'NONE', #36460, .T. ) ;
#65864=EDGE_LOOP ( 'NONE', ( #34045, #36439, #133484, #108882 ) ) ;
#65865=EDGE_LOOP ( 'NONE', ( #34490, #97935, #60719 ) ) ;
#65866=ORIENTED_EDGE ( 'NONE', *, *, #30885, .T. ) ;
#65867=CARTESIAN_POINT ( 'NONE',  ( -0.6932699330959857242, -3.740707523384248390, 12.88036043432867750 ) ) ;
#65868=CARTESIAN_POINT ( 'NONE',  ( -12.18398860626900060, 28.73617430169795739, 5.000000000000000000 ) ) ;
#65869=LINE ( 'NONE', #63192, #53890 ) ;
#65872=DIRECTION ( 'NONE',  ( -0.7071067811865486830, 0.7071067811865464625, 0.000000000000000000 ) ) ;
#65873=LINE ( 'NONE', #131091, #48823 ) ;
#65874=ADVANCED_FACE ( 'NONE', ( #11208 ), #109848, .F. ) ;
#65875=DIRECTION ( 'NONE',  ( -0.000000000000000000, 0.3543493200069153248, 0.9351131265310292928 ) ) ;
#65876=DIRECTION ( 'NONE',  ( 0.7071067811865487940, 0.7071067811865463515, -0.000000000000000000 ) ) ;
#65877=DIRECTION ( 'NONE',  ( -0.6830127018922180770, -0.6830127018922204085, -0.2588190451025213501 ) ) ;
#65878=VERTEX_POINT ( 'NONE', #1753 ) ;
#65879=DIRECTION ( 'NONE',  ( 0.000000000000000000, 0.000000000000000000, -1.000000000000000000 ) ) ;
#65882=LINE ( 'NONE', #53542, #119676 ) ;
#65883=CARTESIAN_POINT ( 'NONE',  ( -20.57672154193634384, 11.25929247661560240, 17.85071094206589137 ) ) ;
#65884=ORIENTED_EDGE ( 'NONE', *, *, #111807, .F. ) ;
#65888=ORIENTED_EDGE ( 'NONE', *, *, #130808, .F. ) ;
#65890=DIRECTION ( 'NONE',  ( 0.7071067811865487940, 0.7071067811865463515, -0.000000000000000000 ) ) ;
#65891=ORIENTED_EDGE ( 'NONE', *, *, #72187, .F. ) ;
#65892=CARTESIAN_POINT ( 'NONE',  ( 0.000000000000000000, 0.000000000000000000, 5.000000000000000000 ) ) ;
#65894=AXIS2_PLACEMENT_3D ( 'NONE', #32759, #31322, #53801 ) ;
#65895=ADVANCED_FACE ( 'NONE', ( #350 ), #1060, .F. ) ;
#65898=ORIENTED_EDGE ( 'NONE', *, *, #28833, .F. ) ;
#65899=DIRECTION ( 'NONE',  ( -0.7071067811865486830, -0.7071067811865464625, -0.000000000000000000 ) ) ;
#65901=VERTEX_POINT ( 'NONE', #45347 ) ;
#65902=ORIENTED_EDGE ( 'NONE', *, *, #90436, .F. ) ;
#65903=LINE ( 'NONE', #109365, #35257 ) ;
#65905=CARTESIAN_POINT ( 'NONE',  ( 39.18398860626899705, 28.73617430169814568, 5.000000000000000000 ) ) ;
#65906=PLANE ( 'NONE',  #88224 ) ;
#65907=AXIS2_PLACEMENT_3D ( 'NONE', #987, #98876, #23470 ) ;
#65912=ORIENTED_EDGE ( 'NONE', *, *, #20473, .T. ) ;
#65913=ORIENTED_EDGE ( 'NONE', *, *, #60517, .T. ) ;
#65914=VECTOR ( 'NONE', #103939, 1000.000000000000000 ) ;
#65915=LINE ( 'NONE', #53586, #45752 ) ;
#65916=VERTEX_POINT ( 'NONE', #58385 ) ;
#65917=ORIENTED_EDGE ( 'NONE', *, *, #83908, .F. ) ;
#65918=CARTESIAN_POINT ( 'NONE',  ( -28.49999999999979039, 4.466399257802221356, 5.000000000000000000 ) ) ;
#65919=ORIENTED_EDGE ( 'NONE', *, *, #40276, .F. ) ;
#65922=CARTESIAN_POINT ( 'NONE',  ( 10.49999999999993250, -1.533600742197719580, 5.000000000000000000 ) ) ;
#65923=LINE ( 'NONE', #9312, #94194 ) ;
#65924=PLANE ( 'NONE',  #15950 ) ;
#65925=LINE ( 'NONE', #142739, #125413 ) ;
#65926=EDGE_LOOP ( 'NONE', ( #37719, #65482, #101436, #48679 ) ) ;
#65927=DIRECTION ( 'NONE',  ( -0.7071067811865487940, 0.7071067811865463515, -0.000000000000000000 ) ) ;
#65928=ORIENTED_EDGE ( 'NONE', *, *, #55929, .T. ) ;
#65929=DIRECTION ( 'NONE',  ( -0.3543493200069162685, -0.000000000000000000, -0.9351131265310288487 ) ) ;
#65930=ORIENTED_EDGE ( 'NONE', *, *, #53365, .T. ) ;
#65932=EDGE_CURVE ( 'NONE', #76747, #134004, #82940, .T. ) ;
#65933=ORIENTED_EDGE ( 'NONE', *, *, #73931, .F. ) ;
#65934=CARTESIAN_POINT ( 'NONE',  ( 5.999999999999956479, -5.527737879153189482, -7.983877177622385801 ) ) ;
#65936=ORIENTED_EDGE ( 'NONE', *, *, #42057, .F. ) ;
#65937=VERTEX_POINT ( 'NONE', #4585 ) ;
#65938=VECTOR ( 'NONE', #65641, 999.9999999999998863 ) ;
#65940=ADVANCED_FACE ( 'NONE', ( #38717 ), #90977, .F. ) ;
#65941=FACE_OUTER_BOUND ( 'NONE', #46700, .T. ) ;
#65942=FACE_OUTER_BOUND ( 'NONE', #64152, .T. ) ;
#65943=AXIS2_PLACEMENT_3D ( 'NONE', #13606, #90487, #77493 ) ;
#65946=LINE ( 'NONE', #75368, #7831 ) ;
#65947=EDGE_CURVE ( 'NONE', #6354, #15312, #6038, .T. ) ;
#65949=DIRECTION ( 'NONE',  ( -4.681814790819591790E-17, -0.3543493200069152693, 0.9351131265310292928 ) ) ;
#65950=VECTOR ( 'NONE', #97035, 1000.000000000000227 ) ;
#65952=LINE ( 'NONE', #86954, #25043 ) ;
#65953=DIRECTION ( 'NONE',  ( -0.6830127018922181881, 0.6830127018922202975, -0.2588190451025214056 ) ) ;
#65954=ADVANCED_FACE ( 'NONE', ( #103243 ), #3212, .F. ) ;
#65956=EDGE_CURVE ( 'NONE', #86472, #73773, #82245, .T. ) ;
#65957=LINE ( 'NONE', #8626, #117697 ) ;
#65958=DIRECTION ( 'NONE',  ( 0.7071067811865487940, 0.7071067811865463515, 0.000000000000000000 ) ) ;
#65960=ORIENTED_EDGE ( 'NONE', *, *, #119759, .F. ) ;
#65961=ORIENTED_EDGE ( 'NONE', *, *, #103126, .F. ) ;
#65963=VERTEX_POINT ( 'NONE', #60497 ) ;
#65964=ORIENTED_EDGE ( 'NONE', *, *, #27572, .F. ) ;
#65965=CARTESIAN_POINT ( 'NONE',  ( 23.67183060077630330, 8.259292476615630818, 4.000000000000000000 ) ) ;
#65967=EDGE_CURVE ( 'NONE', #14576, #15770, #59084, .T. ) ;
#65968=EDGE_CURVE ( 'NONE', #132252, #1839, #102566, .T. ) ;
#65970=LINE ( 'NONE', #98550, #11611 ) ;
#65971=ORIENTED_EDGE ( 'NONE', *, *, #69811, .T. ) ;
#65972=CARTESIAN_POINT ( 'NONE',  ( 17.51078643762690845, -27.52281430457043143, 5.000000000000000000 ) ) ;
#65973=EDGE_LOOP ( 'NONE', ( #6134, #26819, #134444, #41728 ) ) ;
#65975=DIRECTION ( 'NONE',  ( -0.000000000000000000, 0.000000000000000000, 1.000000000000000000 ) ) ;
#65977=EDGE_LOOP ( 'NONE', ( #70537, #117772, #119230, #47303 ) ) ;
#65981=CARTESIAN_POINT ( 'NONE',  ( -16.49999999999988276, -19.91253812416055169, 4.000000000000000000 ) ) ;
#65982=ORIENTED_EDGE ( 'NONE', *, *, #140608, .F. ) ;
#65983=ORIENTED_EDGE ( 'NONE', *, *, #17294, .F. ) ;
#65984=ORIENTED_EDGE ( 'NONE', *, *, #112028, .T. ) ;
#65985=CARTESIAN_POINT ( 'NONE',  ( 48.48921356237309510, -27.52281430457089328, 5.000000000000000000 ) ) ;
#65986=DIRECTION ( 'NONE',  ( 0.6830127018922181881, 0.6830127018922202975, -0.2588190451025214056 ) ) ;
#65987=CARTESIAN_POINT ( 'NONE',  ( 10.49999999999993427, 0.05218569542917404769, 5.000000000000000000 ) ) ;
#65988=DIRECTION ( 'NONE',  ( -0.000000000000000000, -0.3543493200069152693, 0.9351131265310292928 ) ) ;
#65989=CARTESIAN_POINT ( 'NONE',  ( 69.29974487139159578, -27.71228299555254537, 4.000000000000000000 ) ) ;
#65990=VECTOR ( 'NONE', #100847, 1000.000000000000000 ) ;
#65991=ORIENTED_EDGE ( 'NONE', *, *, #47365, .F. ) ;
#65992=LINE ( 'NONE', #142114, #22884 ) ;
#65993=FACE_OUTER_BOUND ( 'NONE', #87552, .T. ) ;
#65994=EDGE_CURVE ( 'NONE', #20842, #71467, #114129, .T. ) ;
#65995=VERTEX_POINT ( 'NONE', #16964 ) ;
#65996=DIRECTION ( 'NONE',  ( 1.000000000000000000, 0.000000000000000000, 0.000000000000000000 ) ) ;
#65997=FACE_OUTER_BOUND ( 'NONE', #115974, .T. ) ;
#66000=ORIENTED_EDGE ( 'NONE', *, *, #126909, .F. ) ;
#66001=EDGE_LOOP ( 'NONE', ( #43793, #120474, #20120, #5864 ) ) ;
#66003=CARTESIAN_POINT ( 'NONE',  ( 7.499999999999947597, -17.56887692260763245, 4.000000000000000000 ) ) ;
#66004=ORIENTED_EDGE ( 'NONE', *, *, #117489, .T. ) ;
#66005=DIRECTION ( 'NONE',  ( -0.000000000000000000, 0.000000000000000000, 1.000000000000000000 ) ) ;
#66006=EDGE_CURVE ( 'NONE', #78277, #48269, #14815, .T. ) ;
#66008=DIRECTION ( 'NONE',  ( 2.781805975412906507E-17, 0.3543493200069153248, 0.9351131265310292928 ) ) ;
#66009=DIRECTION ( 'NONE',  ( 0.7071067811865487940, 0.7071067811865463515, -0.000000000000000000 ) ) ;
#66010=CARTESIAN_POINT ( 'NONE',  ( -14.99999999999988987, -12.03360074219761522, 5.000000000000000000 ) ) ;
#66011=EDGE_CURVE ( 'NONE', #6847, #7168, #124294, .T. ) ;
#66012=CARTESIAN_POINT ( 'NONE',  ( 34.92499999999998295, -10.65190338184899410, -7.458287694568761950 ) ) ;
#66013=DIRECTION ( 'NONE',  ( 0.7071067811865487940, 0.7071067811865463515, -0.000000000000000000 ) ) ;
#66014=CARTESIAN_POINT ( 'NONE',  ( 36.48921356237310221, -27.52281430457080802, 5.000000000000000000 ) ) ;
#66015=LINE ( 'NONE', #107337, #142890 ) ;
#66016=LINE ( 'NONE', #109487, #120877 ) ;
#66017=CARTESIAN_POINT ( 'NONE',  ( 30.29974487139158867, -27.71228299555227537, 4.000000000000000000 ) ) ;
#66018=DIRECTION ( 'NONE',  ( 0.6830127018922180770, -0.6830127018922204085, -0.2588190451025214056 ) ) ;
#66019=CARTESIAN_POINT ( 'NONE',  ( -34.42500000000001137, 21.72500000000000142, 0.5000000000000000000 ) ) ;
#66020=VERTEX_POINT ( 'NONE', #70667 ) ;
#66021=VERTEX_POINT ( 'NONE', #3890 ) ;
#66023=ORIENTED_EDGE ( 'NONE', *, *, #122884, .T. ) ;
#66024=VECTOR ( 'NONE', #56580, 1000.000000000000000 ) ;
#66025=ORIENTED_EDGE ( 'NONE', *, *, #42537, .F. ) ;
#66026=ADVANCED_FACE ( 'NONE', ( #125741 ), #114810, .F. ) ;
#66027=VERTEX_POINT ( 'NONE', #48890 ) ;
#66028=DIRECTION ( 'NONE',  ( -0.7071067811865486830, -0.7071067811865464625, -0.000000000000000000 ) ) ;
#66030=ORIENTED_EDGE ( 'NONE', *, *, #85208, .F. ) ;
#66032=CARTESIAN_POINT ( 'NONE',  ( 27.48921356237309155, -27.52281430457074762, 5.000000000000000000 ) ) ;
#66033=CARTESIAN_POINT ( 'NONE',  ( -75.48921356237309510, -27.52281430457107803, 5.000000000000000000 ) ) ;
#66034=LINE ( 'NONE', #77618, #127632 ) ;
#66035=EDGE_CURVE ( 'NONE', #13073, #6949, #104676, .T. ) ;
#66036=ORIENTED_EDGE ( 'NONE', *, *, #92222, .T. ) ;
#66037=CARTESIAN_POINT ( 'NONE',  ( 29.29289321881326202, -18.74070752338408852, 5.000000000000000000 ) ) ;
#66038=FACE_OUTER_BOUND ( 'NONE', #13264, .T. ) ;
#66039=PLANE ( 'NONE',  #112278 ) ;
#66040=PLANE ( 'NONE',  #42269 ) ;
#66042=DIRECTION ( 'NONE',  ( -0.3543493200069163240, -0.000000000000000000, -0.9351131265310288487 ) ) ;
#66045=ORIENTED_EDGE ( 'NONE', *, *, #9311, .F. ) ;
#66046=VERTEX_POINT ( 'NONE', #138032 ) ;
#66047=AXIS2_PLACEMENT_3D ( 'NONE', #122246, #88953, #133862 ) ;
#66049=ORIENTED_EDGE ( 'NONE', *, *, #1984, .F. ) ;
#66050=VECTOR ( 'NONE', #134044, 1000.000000000000000 ) ;
#66051=LINE ( 'NONE', #110213, #99529 ) ;
#66052=CARTESIAN_POINT ( 'NONE',  ( 13.49999999999990408, 21.43112307739196609, 4.000000000000000000 ) ) ;
#66053=DIRECTION ( 'NONE',  ( -0.6830127018922180770, 0.6830127018922202975, -0.2588190451025213501 ) ) ;
#66054=CARTESIAN_POINT ( 'NONE',  ( 21.99507522778792534, -5.240707523384225297, 12.38332538355491153 ) ) ;
#66059=EDGE_LOOP ( 'NONE', ( #59135, #20123, #47877, #30380 ) ) ;
#66060=VERTEX_POINT ( 'NONE', #50314 ) ;
#66061=CARTESIAN_POINT ( 'NONE',  ( -15.18398860626900237, 28.73617430169797871, 5.000000000000000000 ) ) ;
#66062=CARTESIAN_POINT ( 'NONE',  ( -57.48921356237308800, -27.52281430457095368, 5.000000000000000000 ) ) ;
#66063=ORIENTED_EDGE ( 'NONE', *, *, #34345, .F. ) ;
#66066=ORIENTED_EDGE ( 'NONE', *, *, #7467, .T. ) ;
#66067=DIRECTION ( 'NONE',  ( 1.000000000000000000, 0.000000000000000000, 0.000000000000000000 ) ) ;
#66068=EDGE_CURVE ( 'NONE', #114249, #74087, #108207, .T. ) ;
#66070=CARTESIAN_POINT ( 'NONE',  ( -6.489213562373093325, -27.52281430457059841, 5.000000000000000000 ) ) ;
#66072=ORIENTED_EDGE ( 'NONE', *, *, #131863, .F. ) ;
#66073=CARTESIAN_POINT ( 'NONE',  ( -2.700255128608413990, -27.71228299555204089, 4.000000000000000000 ) ) ;
#66074=EDGE_LOOP ( 'NONE', ( #139963, #20631, #132571, #15906 ) ) ;
#66075=ORIENTED_EDGE ( 'NONE', *, *, #81494, .T. ) ;
#66076=ORIENTED_EDGE ( 'NONE', *, *, #22875, .T. ) ;
#66077=DIRECTION ( 'NONE',  ( -0.7071067811865486830, 0.7071067811865464625, 0.000000000000000000 ) ) ;
#66079=ORIENTED_EDGE ( 'NONE', *, *, #109956, .F. ) ;
#66080=LINE ( 'NONE', #21838, #22785 ) ;
#66081=CARTESIAN_POINT ( 'NONE',  ( -10.49999999999993250, 5.696342897626490931, -7.587980461218421624 ) ) ;
#66083=FACE_OUTER_BOUND ( 'NONE', #120172, .T. ) ;
#66084=FACE_BOUND ( 'NONE', #30198, .T. ) ;
#66085=ORIENTED_EDGE ( 'NONE', *, *, #19303, .F. ) ;
#66086=CARTESIAN_POINT ( 'NONE',  ( -32.20710678118632586, 15.75929247661555443, 5.000000000000000000 ) ) ;
#66087=LINE ( 'NONE', #134192, #120794 ) ;
#66088=CARTESIAN_POINT ( 'NONE',  ( -15.29974487139158867, -27.71228299555216879, 4.000000000000000000 ) ) ;
#66089=ORIENTED_EDGE ( 'NONE', *, *, #59410, .F. ) ;
#66091=ORIENTED_EDGE ( 'NONE', *, *, #76096, .F. ) ;
#66092=VERTEX_POINT ( 'NONE', #94502 ) ;
#66093=LINE ( 'NONE', #110262, #104977 ) ;
#66098=ORIENTED_EDGE ( 'NONE', *, *, #107842, .F. ) ;
#66099=CARTESIAN_POINT ( 'NONE',  ( 31.49999999999977973, 3.431123077392151277, 4.000000000000000000 ) ) ;
#66100=EDGE_CURVE ( 'NONE', #1472, #105971, #119119, .T. ) ;
#66101=FACE_OUTER_BOUND ( 'NONE', #38321, .T. ) ;
#66102=LINE ( 'NONE', #120416, #37194 ) ;
#66103=VERTEX_POINT ( 'NONE', #53135 ) ;
#66105=CARTESIAN_POINT ( 'NONE',  ( 0.5166543864104510275, 22.22500000000000142, 4.500000000000000888 ) ) ;
#66106=CARTESIAN_POINT ( 'NONE',  ( -27.18398860626900060, 28.73617430169806042, 5.000000000000000000 ) ) ;
#66107=ADVANCED_FACE ( 'NONE', ( #52428 ), #19800, .F. ) ;
#66109=FACE_OUTER_BOUND ( 'NONE', #98240, .T. ) ;
#66110=VECTOR ( 'NONE', #112181, 1000.000000000000227 ) ;
#66111=DIRECTION ( 'NONE',  ( 0.7071067811865486830, -0.7071067811865464625, -0.000000000000000000 ) ) ;
#66113=LINE ( 'NONE', #87133, #74892 ) ;
#66114=DIRECTION ( 'NONE',  ( 0.7071067811865487940, 0.7071067811865463515, 0.000000000000000000 ) ) ;
#66115=ORIENTED_EDGE ( 'NONE', *, *, #62687, .T. ) ;
#66116=ORIENTED_EDGE ( 'NONE', *, *, #124525, .F. ) ;
#66117=ORIENTED_EDGE ( 'NONE', *, *, #42, .F. ) ;
#66118=DIRECTION ( 'NONE',  ( -0.7071067811865486830, -0.7071067811865464625, 0.000000000000000000 ) ) ;
#66119=CARTESIAN_POINT ( 'NONE',  ( -14.01844734635661283, 18.75929247661553134, 20.33588619593446367 ) ) ;
#66120=VERTEX_POINT ( 'NONE', #117659 ) ;
#66121=ORIENTED_EDGE ( 'NONE', *, *, #61115, .T. ) ;
#66122=CARTESIAN_POINT ( 'NONE',  ( 2.510786437626908008, -27.52281430457053446, 5.000000000000000000 ) ) ;
#66123=FACE_OUTER_BOUND ( 'NONE', #83563, .T. ) ;
#66124=EDGE_CURVE ( 'NONE', #76368, #27605, #97340, .T. ) ;
#66125=EDGE_CURVE ( 'NONE', #121862, #109240, #75634, .T. ) ;
#66126=CARTESIAN_POINT ( 'NONE',  ( 4.499999999999974243, -1.533600742197722910, 5.000000000000000000 ) ) ;
#66127=EDGE_LOOP ( 'NONE', ( #18018, #113455, #90011, #60073 ) ) ;
#66128=LINE ( 'NONE', #32790, #67190 ) ;
#66129=ADVANCED_FACE ( 'NONE', ( #40178 ), #138753, .F. ) ;
#66130=VECTOR ( 'NONE', #47865, 1000.000000000000000 ) ;
#66133=AXIS2_PLACEMENT_3D ( 'NONE', #49985, #25352, #16611 ) ;
#66134=CARTESIAN_POINT ( 'NONE',  ( 5.510786437626906675, -27.52281430457051314, 5.000000000000000000 ) ) ;
#66135=ORIENTED_EDGE ( 'NONE', *, *, #124140, .T. ) ;
#66137=VECTOR ( 'NONE', #15756, 1000.000000000000227 ) ;
#66138=LINE ( 'NONE', #131379, #116045 ) ;
#66139=LINE ( 'NONE', #35673, #58924 ) ;
#66140=EDGE_CURVE ( 'NONE', #28852, #111481, #39450, .T. ) ;
#66143=DIRECTION ( 'NONE',  ( 1.000000000000000000, 0.000000000000000000, 0.000000000000000000 ) ) ;
#66144=ORIENTED_EDGE ( 'NONE', *, *, #34171, .T. ) ;
#66145=CARTESIAN_POINT ( 'NONE',  ( -14.51078643762690490, -27.52281430457045275, 5.000000000000000000 ) ) ;
#66146=CARTESIAN_POINT ( 'NONE',  ( -28.18992724054673360, -22.22500000000000142, 7.552170838797634289 ) ) ;
#66147=LINE ( 'NONE', #123392, #61187 ) ;
#66148=EDGE_LOOP ( 'NONE', ( #86093, #134114, #119362 ) ) ;
#66149=CARTESIAN_POINT ( 'NONE',  ( -8.207106781186482181, -14.24070752338413826, 5.000000000000000000 ) ) ;
#66150=CARTESIAN_POINT ( 'NONE',  ( 1.499999999999990896, -2.173586137069138946, -4.605770156576107333 ) ) ;
#66151=ADVANCED_FACE ( 'NONE', ( #119807 ), #83677, .F. ) ;
#66153=CARTESIAN_POINT ( 'NONE',  ( -77.99451991528749772, 28.92564299267992567, 4.000000000000000000 ) ) ;
#66154=DIRECTION ( 'NONE',  ( 2.781805975412906507E-17, 0.3543493200069153248, 0.9351131265310292928 ) ) ;
#66155=ORIENTED_EDGE ( 'NONE', *, *, #22875, .F. ) ;
#66156=CARTESIAN_POINT ( 'NONE',  ( 19.49999999999986500, 16.77039438581780928, 0.4657186855307289264 ) ) ;
#66157=DIRECTION ( 'NONE',  ( 0.7071067811865487940, 0.7071067811865463515, 0.000000000000000000 ) ) ;
#66158=EDGE_LOOP ( 'NONE', ( #36862, #124873, #54003, #22157 ) ) ;
#66159=ORIENTED_EDGE ( 'NONE', *, *, #120953, .F. ) ;
#66160=CARTESIAN_POINT ( 'NONE',  ( -22.49999999999984723, -15.29013452822856323, 0.3645803511609828629 ) ) ;
#66161=CARTESIAN_POINT ( 'NONE',  ( -4.499999999999968914, -4.216083040037257312, -7.486842126848645584 ) ) ;
#66163=EDGE_CURVE ( 'NONE', #89577, #127256, #51748, .T. ) ;
#66164=LINE ( 'NONE', #111038, #143114 ) ;
#66165=CARTESIAN_POINT ( 'NONE',  ( -32.99999999999976552, 13.93112307739204248, 4.000000000000000000 ) ) ;
#66166=DIRECTION ( 'NONE',  ( 0.7071067811865487940, 0.7071067811865463515, 0.000000000000000000 ) ) ;
#66167=EDGE_LOOP ( 'NONE', ( #27247, #27831, #33068, #68695 ) ) ;
#66169=EDGE_CURVE ( 'NONE', #91146, #5100, #129272, .T. ) ;
#66170=DIRECTION ( 'NONE',  ( -0.000000000000000000, 0.000000000000000000, 1.000000000000000000 ) ) ;
#66171=CARTESIAN_POINT ( 'NONE',  ( -10.49999999999992539, -11.56887692260769640, 4.000000000000000000 ) ) ;
#66172=CARTESIAN_POINT ( 'NONE',  ( -74.99451991528749772, 28.92564299267990435, 4.000000000000000000 ) ) ;
#66176=ORIENTED_EDGE ( 'NONE', *, *, #69709, .T. ) ;
#66178=ORIENTED_EDGE ( 'NONE', *, *, #130929, .T. ) ;
#66180=ORIENTED_EDGE ( 'NONE', *, *, #125148, .F. ) ;
#66181=CARTESIAN_POINT ( 'NONE',  ( 31.49999999999977263, -12.08601207473287253, -10.46905243149102027 ) ) ;
#66182=CARTESIAN_POINT ( 'NONE',  ( -14.29289321881335262, -9.740707523384180888, 5.000000000000000000 ) ) ;
#66183=EDGE_LOOP ( 'NONE', ( #49921, #97801, #126533, #17481 ) ) ;
#66184=LINE ( 'NONE', #11031, #46291 ) ;
#66185=CARTESIAN_POINT ( 'NONE',  ( 18.70710678118641468, 14.25929247661557042, 5.000000000000000000 ) ) ;
#66187=LINE ( 'NONE', #24102, #95119 ) ;
#66189=ADVANCED_FACE ( 'NONE', ( #30716 ), #20498, .F. ) ;
#66190=EDGE_LOOP ( 'NONE', ( #18995, #103541, #116628, #70915 ) ) ;
#66191=DIRECTION ( 'NONE',  ( -0.7071067811865486830, -0.7071067811865464625, -0.000000000000000000 ) ) ;
#66193=FACE_OUTER_BOUND ( 'NONE', #8179, .T. ) ;
#66194=DIRECTION ( 'NONE',  ( -0.7071067811865487940, 0.7071067811865463515, -0.000000000000000000 ) ) ;
#66195=PLANE ( 'NONE',  #89077 ) ;
#66196=DIRECTION ( 'NONE',  ( -0.3543493200069162685, -0.000000000000000000, -0.9351131265310288487 ) ) ;
#66199=VECTOR ( 'NONE', #86190, 1000.000000000000000 ) ;
#66200=DIRECTION ( 'NONE',  ( 2.781805975412906507E-17, 0.3543493200069153248, 0.9351131265310292928 ) ) ;
#66201=LINE ( 'NONE', #132175, #92371 ) ;
#66202=ORIENTED_EDGE ( 'NONE', *, *, #88190, .T. ) ;
#66203=ORIENTED_EDGE ( 'NONE', *, *, #126556, .T. ) ;
#66205=VECTOR ( 'NONE', #82285, 1000.000000000000000 ) ;
#66206=CARTESIAN_POINT ( 'NONE',  ( -34.42500000000001137, -10.45860074219788416, 5.000000000000000000 ) ) ;
#66207=CARTESIAN_POINT ( 'NONE',  ( -32.99451991528749062, 28.92564299267960948, 4.000000000000000000 ) ) ;
#66208=ORIENTED_EDGE ( 'NONE', *, *, #140571, .T. ) ;
#66209=PLANE ( 'NONE',  #57150 ) ;
#66210=LINE ( 'NONE', #42323, #76970 ) ;
#66212=ADVANCED_FACE ( 'NONE', ( #21946 ), #21238, .F. ) ;
#66213=AXIS2_PLACEMENT_3D ( 'NONE', #59769, #70663, #3887 ) ;
#66214=ORIENTED_EDGE ( 'NONE', *, *, #19912, .F. ) ;
#66215=FACE_OUTER_BOUND ( 'NONE', #79528, .T. ) ;
#66216=ORIENTED_EDGE ( 'NONE', *, *, #7630, .F. ) ;
#66217=EDGE_LOOP ( 'NONE', ( #27754, #141187, #137734, #102865 ) ) ;
#66218=FACE_OUTER_BOUND ( 'NONE', #87174, .T. ) ;
#66219=DIRECTION ( 'NONE',  ( -0.000000000000000000, 0.3543493200069153248, 0.9351131265310292928 ) ) ;
#66220=CARTESIAN_POINT ( 'NONE',  ( -8.843876922607519120, -22.22500000000000497, 4.000000000000000000 ) ) ;
#66221=CARTESIAN_POINT ( 'NONE',  ( -27.18398860626900060, 28.73617430169806042, 5.000000000000000000 ) ) ;
#66224=LINE ( 'NONE', #109708, #90539 ) ;
#66226=ORIENTED_EDGE ( 'NONE', *, *, #16802, .F. ) ;
#66229=FACE_OUTER_BOUND ( 'NONE', #46932, .T. ) ;
#66230=CARTESIAN_POINT ( 'NONE',  ( 0.000000000000000000, 0.000000000000000000, 5.000000000000000000 ) ) ;
#66231=FACE_OUTER_BOUND ( 'NONE', #70688, .T. ) ;
#66232=CARTESIAN_POINT ( 'NONE',  ( 0.000000000000000000, 0.000000000000000000, 5.000000000000000000 ) ) ;
#66233=VECTOR ( 'NONE', #94534, 1000.000000000000000 ) ;
#66234=VECTOR ( 'NONE', #142353, 1000.000000000000000 ) ;
#66235=ORIENTED_EDGE ( 'NONE', *, *, #9246, .F. ) ;
#66236=DIRECTION ( 'NONE',  ( -0.7071067811865486830, -0.7071067811865464625, -0.000000000000000000 ) ) ;
#66240=CARTESIAN_POINT ( 'NONE',  ( 15.29974487139158867, -27.71228299555216879, 4.000000000000000000 ) ) ;
#66241=ORIENTED_EDGE ( 'NONE', *, *, #125676, .T. ) ;
#66242=ORIENTED_EDGE ( 'NONE', *, *, #54143, .F. ) ;
#66243=VECTOR ( 'NONE', #136398, 1000.000000000000000 ) ;
#66244=DIRECTION ( 'NONE',  ( 0.7071067811865487940, -0.7071067811865463515, 0.000000000000000000 ) ) ;
#66246=VERTEX_POINT ( 'NONE', #121957 ) ;
#66247=EDGE_CURVE ( 'NONE', #32991, #87440, #44456, .T. ) ;
#66248=CARTESIAN_POINT ( 'NONE',  ( -34.92500000000001137, 15.00612307739177709, 4.000000000000000000 ) ) ;
#66249=ORIENTED_EDGE ( 'NONE', *, *, #24865, .F. ) ;
#66250=PLANE ( 'NONE',  #134913 ) ;
#66251=DIRECTION ( 'NONE',  ( -0.7071067811865487940, 0.7071067811865463515, 0.000000000000000000 ) ) ;
#66252=CARTESIAN_POINT ( 'NONE',  ( -1.499999999999987788, -19.91253812416055524, 4.000000000000000000 ) ) ;
#66253=FACE_BOUND ( 'NONE', #8656, .T. ) ;
#66254=DIRECTION ( 'NONE',  ( 0.7071067811865487940, 0.7071067811865463515, -0.000000000000000000 ) ) ;
#66255=CARTESIAN_POINT ( 'NONE',  ( -4.499999999999974243, 21.43112307739196964, 4.000000000000000000 ) ) ;
#66256=DIRECTION ( 'NONE',  ( 0.7071067811865487940, 0.7071067811865463515, 0.000000000000000000 ) ) ;
#66257=PLANE ( 'NONE',  #8611 ) ;
#66258=LINE ( 'NONE', #8253, #82875 ) ;
#66259=ORIENTED_EDGE ( 'NONE', *, *, #131848, .T. ) ;
#66262=VERTEX_POINT ( 'NONE', #34266 ) ;
#66263=EDGE_CURVE ( 'NONE', #22970, #90775, #123449, .T. ) ;
#66264=EDGE_LOOP ( 'NONE', ( #13689, #58804, #133224, #68370 ) ) ;
#66266=ORIENTED_EDGE ( 'NONE', *, *, #11695, .F. ) ;
#66267=DIRECTION ( 'NONE',  ( -0.000000000000000000, 0.3543493200069153248, 0.9351131265310292928 ) ) ;
#66269=CARTESIAN_POINT ( 'NONE',  ( 31.49999999999977263, 16.08746187583908949, 4.000000000000000000 ) ) ;
#66270=EDGE_CURVE ( 'NONE', #136439, #106829, #46863, .T. ) ;
#66272=PLANE ( 'NONE',  #72282 ) ;
#66273=EDGE_CURVE ( 'NONE', #97224, #94242, #22628, .T. ) ;
#66274=EDGE_CURVE ( 'NONE', #109576, #111037, #32119, .T. ) ;
#66275=CARTESIAN_POINT ( 'NONE',  ( 30.77004279457771574, 21.73644205237998150, 5.000000000000000888 ) ) ;
#66276=DIRECTION ( 'NONE',  ( 0.7071067811865487940, 0.7071067811865463515, -0.000000000000000000 ) ) ;
#66278=CARTESIAN_POINT ( 'NONE',  ( -6.328169399223490643, 5.259292476615663681, 4.000000000000000000 ) ) ;
#66280=FACE_OUTER_BOUND ( 'NONE', #10489, .T. ) ;
#66281=VERTEX_POINT ( 'NONE', #66894 ) ;
#66282=VECTOR ( 'NONE', #22099, 1000.000000000000000 ) ;
#66283=DIRECTION ( 'NONE',  ( -0.000000000000000000, 0.3543493200069153248, 0.9351131265310292928 ) ) ;
#66285=DIRECTION ( 'NONE',  ( 0.7071067811865486830, -0.7071067811865464625, -0.000000000000000000 ) ) ;
#66286=ORIENTED_EDGE ( 'NONE', *, *, #31110, .F. ) ;
#66287=ORIENTED_EDGE ( 'NONE', *, *, #124678, .F. ) ;
#66288=DIRECTION ( 'NONE',  ( 0.7071067811865486830, -0.7071067811865464625, -0.000000000000000000 ) ) ;
#66289=EDGE_CURVE ( 'NONE', #110269, #128513, #45177, .T. ) ;
#66290=EDGE_CURVE ( 'NONE', #92018, #3467, #61649, .T. ) ;
#66291=PLANE ( 'NONE',  #127220 ) ;
#66292=ORIENTED_EDGE ( 'NONE', *, *, #101358, .T. ) ;
#66295=AXIS2_PLACEMENT_3D ( 'NONE', #59165, #89604, #122218 ) ;
#66296=LINE ( 'NONE', #110468, #30475 ) ;
#66299=EDGE_CURVE ( 'NONE', #40076, #85488, #56776, .T. ) ;
#66302=PLANE ( 'NONE',  #80437 ) ;
#66303=ORIENTED_EDGE ( 'NONE', *, *, #55831, .T. ) ;
#66304=CARTESIAN_POINT ( 'NONE',  ( -26.99999999999981526, 7.931123077392106424, 4.000000000000000000 ) ) ;
#66305=CARTESIAN_POINT ( 'NONE',  ( 0.000000000000000000, -21.72500000000000142, 4.500000000000000888 ) ) ;
#66306=ADVANCED_FACE ( 'NONE', ( #109674 ), #13908, .F. ) ;
#66307=PLANE ( 'NONE',  #118859 ) ;
#66308=VERTEX_POINT ( 'NONE', #103769 ) ;
#66309=VERTEX_POINT ( 'NONE', #91511 ) ;
#66310=DIRECTION ( 'NONE',  ( -0.7071067811865486830, -0.7071067811865464625, 0.000000000000000000 ) ) ;
#66311=CARTESIAN_POINT ( 'NONE',  ( 6.489213562373093325, -27.52281430457059841, 5.000000000000000000 ) ) ;
#66312=PLANE ( 'NONE',  #104994 ) ;
#66313=ORIENTED_EDGE ( 'NONE', *, *, #138809, .T. ) ;
#66315=EDGE_LOOP ( 'NONE', ( #110162, #118325, #24669 ) ) ;
#66316=VECTOR ( 'NONE', #53405, 1000.000000000000114 ) ;
#66317=CARTESIAN_POINT ( 'NONE',  ( -34.42500000000001137, 13.54139925780187603, 5.000000000000000000 ) ) ;
#66320=EDGE_CURVE ( 'NONE', #14802, #11535, #37855, .T. ) ;
#66321=DIRECTION ( 'NONE',  ( -0.000000000000000000, 0.3543493200069153248, 0.9351131265310292928 ) ) ;
#66324=CARTESIAN_POINT ( 'NONE',  ( 0.000000000000000000, 0.000000000000000000, 5.000000000000000000 ) ) ;
#66327=EDGE_LOOP ( 'NONE', ( #36757, #109710, #22549, #93667 ) ) ;
#66328=CARTESIAN_POINT ( 'NONE',  ( 8.994519915287490619, 28.92564299267944250, 4.000000000000000000 ) ) ;
#66329=ADVANCED_FACE ( 'NONE', ( #124836 ), #125570, .F. ) ;
#66330=VERTEX_POINT ( 'NONE', #27653 ) ;
#66331=EDGE_CURVE ( 'NONE', #108671, #113821, #48715, .T. ) ;
#66332=DIRECTION ( 'NONE',  ( 0.7071067811865486830, -0.7071067811865464625, -0.000000000000000000 ) ) ;
#66334=VECTOR ( 'NONE', #137205, 1000.000000000000114 ) ;
#66335=ADVANCED_FACE ( 'NONE', ( #115343 ), #47342, .F. ) ;
#66337=CARTESIAN_POINT ( 'NONE',  ( 8.999999999999937828, 10.93112307739207267, 4.000000000000000000 ) ) ;
#66338=VECTOR ( 'NONE', #3351, 1000.000000000000227 ) ;
#66340=CARTESIAN_POINT ( 'NONE',  ( -34.92500000000001137, -5.143876922607502955, 4.000000000000000000 ) ) ;
#66341=DIRECTION ( 'NONE',  ( 0.3543493200069162685, -0.000000000000000000, -0.9351131265310288487 ) ) ;
#66342=CARTESIAN_POINT ( 'NONE',  ( -11.51078643762690490, -27.52281430457047406, 5.000000000000000000 ) ) ;
#66343=ORIENTED_EDGE ( 'NONE', *, *, #97819, .T. ) ;
#66346=LINE ( 'NONE', #88085, #16836 ) ;
#66347=CARTESIAN_POINT ( 'NONE',  ( 4.828169399223496860, -5.240707523384231514, 4.000000000000000000 ) ) ;
#66349=DIRECTION ( 'NONE',  ( -0.7071067811865486830, 0.7071067811865464625, 0.000000000000000000 ) ) ;
#66350=DIRECTION ( 'NONE',  ( -0.7071067811865486830, -0.7071067811865464625, -0.000000000000000000 ) ) ;
#66351=CARTESIAN_POINT ( 'NONE',  ( -13.82816939922344091, 9.759292476615621936, 4.000000000000000000 ) ) ;
#66353=EDGE_LOOP ( 'NONE', ( #131978, #110533, #3067, #137335 ) ) ;
#66354=LINE ( 'NONE', #101091, #106740 ) ;
#66355=ORIENTED_EDGE ( 'NONE', *, *, #42869, .T. ) ;
#66356=DIRECTION ( 'NONE',  ( -0.000000000000000000, -0.3543493200069152693, 0.9351131265310292928 ) ) ;
#66357=FACE_OUTER_BOUND ( 'NONE', #127908, .T. ) ;
#66361=DIRECTION ( 'NONE',  ( -0.7071067811865486830, 0.7071067811865464625, 0.000000000000000000 ) ) ;
#66363=ORIENTED_EDGE ( 'NONE', *, *, #141278, .F. ) ;
#66364=CARTESIAN_POINT ( 'NONE',  ( -7.251544128675710965, -11.24070752338417201, 10.39518518046010698 ) ) ;
#66367=CARTESIAN_POINT ( 'NONE',  ( -24.29974487139158867, -27.71228299555223273, 4.000000000000000000 ) ) ;
#66368=DIRECTION ( 'NONE',  ( -0.000000000000000000, -0.3543493200069152693, 0.9351131265310292928 ) ) ;
#66370=FACE_OUTER_BOUND ( 'NONE', #82733, .T. ) ;
#66373=ORIENTED_EDGE ( 'NONE', *, *, #29910, .T. ) ;
#66375=DIRECTION ( 'NONE',  ( 0.6830127018922181881, 0.6830127018922202975, -0.2588190451025214056 ) ) ;
#66376=CARTESIAN_POINT ( 'NONE',  ( -0.3281693992235185098, 5.259292476615672562, 4.000000000000000000 ) ) ;
#66377=LINE ( 'NONE', #68532, #40565 ) ;
#66378=VECTOR ( 'NONE', #14493, 1000.000000000000000 ) ;
#66379=VERTEX_POINT ( 'NONE', #137153 ) ;
#66380=CARTESIAN_POINT ( 'NONE',  ( -33.48921356237309510, -27.52281430457078670, 5.000000000000000000 ) ) ;
#66381=ORIENTED_EDGE ( 'NONE', *, *, #57929, .F. ) ;
#66382=LINE ( 'NONE', #22128, #88212 ) ;
#66384=DIRECTION ( 'NONE',  ( 0.6830127018922180770, -0.6830127018922204085, -0.2588190451025213501 ) ) ;
#66385=VECTOR ( 'NONE', #74928, 1000.000000000000000 ) ;
#66387=CARTESIAN_POINT ( 'NONE',  ( 8.816011393731004731, 28.73617430169781173, 5.000000000000000000 ) ) ;
#66388=LINE ( 'NONE', #87424, #26790 ) ;
#66390=VECTOR ( 'NONE', #63065, 1000.000000000000227 ) ;
#66391=CARTESIAN_POINT ( 'NONE',  ( -24.28001967989388632, 0.7592924766157104211, 14.27032725228003329 ) ) ;
#66392=EDGE_CURVE ( 'NONE', #130071, #137119, #25510, .T. ) ;
#66394=CARTESIAN_POINT ( 'NONE',  ( -14.99999999999990230, -0.2811185226894407085, -5.995736974527478225 ) ) ;
#66395=VERTEX_POINT ( 'NONE', #37110 ) ;
#66396=ADVANCED_FACE ( 'NONE', ( #136416 ), #82090, .F. ) ;
#66397=CARTESIAN_POINT ( 'NONE',  ( 48.18398860626899705, 28.73617430169820608, 5.000000000000000000 ) ) ;
#66398=PLANE ( 'NONE',  #137939 ) ;
#66400=DIRECTION ( 'NONE',  ( 0.7071067811865487940, -0.7071067811865463515, 0.000000000000000000 ) ) ;
#66401=ORIENTED_EDGE ( 'NONE', *, *, #55235, .F. ) ;
#66405=EDGE_LOOP ( 'NONE', ( #68061, #42791, #109592, #116943 ) ) ;
#66407=ADVANCED_FACE ( 'NONE', ( #35734 ), #60325, .F. ) ;
#66408=DIRECTION ( 'NONE',  ( 0.3543493200069162685, -0.000000000000000000, -0.9351131265310288487 ) ) ;
#66409=LINE ( 'NONE', #112050, #17882 ) ;
#66410=CARTESIAN_POINT ( 'NONE',  ( 0.000000000000000000, -21.72500000000000142, 4.500000000000000888 ) ) ;
#66412=DIRECTION ( 'NONE',  ( -0.7071067811865486830, -0.7071067811865464625, 0.000000000000000000 ) ) ;
#66414=EDGE_LOOP ( 'NONE', ( #58622, #44708, #11609, #101249 ) ) ;
#66415=CARTESIAN_POINT ( 'NONE',  ( 6.005480084712508493, 28.92564299267933947, 4.000000000000000000 ) ) ;
#66418=VERTEX_POINT ( 'NONE', #14653 ) ;
#66419=DIRECTION ( 'NONE',  ( -0.3543493200069162685, -0.000000000000000000, -0.9351131265310288487 ) ) ;
#66420=DIRECTION ( 'NONE',  ( 0.7071067811865486830, -0.7071067811865464625, -0.000000000000000000 ) ) ;
#66421=CARTESIAN_POINT ( 'NONE',  ( -5.207106781186495503, -20.24070752338407431, 5.000000000000000000 ) ) ;
#66422=EDGE_CURVE ( 'NONE', #117563, #90351, #56160, .T. ) ;
#66423=ORIENTED_EDGE ( 'NONE', *, *, #64767, .T. ) ;
#66424=VECTOR ( 'NONE', #17011, 1000.000000000000000 ) ;
#66425=FACE_BOUND ( 'NONE', #77552, .T. ) ;
#66426=CARTESIAN_POINT ( 'NONE',  ( -34.92500000000001137, -22.22500000000000142, 4.000000000000000000 ) ) ;
#66427=CARTESIAN_POINT ( 'NONE',  ( -18.29974487139159223, -27.71228299555219010, 4.000000000000000000 ) ) ;
#66428=DIRECTION ( 'NONE',  ( 1.000000000000000000, 0.000000000000000000, 0.000000000000000000 ) ) ;
#66429=EDGE_CURVE ( 'NONE', #72171, #4761, #3727, .T. ) ;
#66432=VECTOR ( 'NONE', #99357, 1000.000000000000227 ) ;
#66434=ORIENTED_EDGE ( 'NONE', *, *, #141453, .T. ) ;
#66435=VECTOR ( 'NONE', #117160, 1000.000000000000000 ) ;
#66436=EDGE_LOOP ( 'NONE', ( #3617, #47671, #129170, #5889 ) ) ;
#66438=ORIENTED_EDGE ( 'NONE', *, *, #119900, .T. ) ;
#66439=ORIENTED_EDGE ( 'NONE', *, *, #24351, .F. ) ;
#66440=EDGE_CURVE ( 'NONE', #123646, #141302, #15326, .T. ) ;
#66441=VECTOR ( 'NONE', #99148, 1000.000000000000000 ) ;
#66442=VECTOR ( 'NONE', #72682, 1000.000000000000000 ) ;
#66443=LINE ( 'NONE', #22181, #21527 ) ;
#66444=CARTESIAN_POINT ( 'NONE',  ( -9.489213562373095101, -27.52281430457062328, 5.000000000000000000 ) ) ;
#66445=ADVANCED_FACE ( 'NONE', ( #6577 ), #107363, .F. ) ;
#66446=ADVANCED_FACE ( 'NONE', ( #139321 ), #110025, .F. ) ;
#66447=DIRECTION ( 'NONE',  ( 0.000000000000000000, -1.000000000000000000, 0.000000000000000000 ) ) ;
#66448=EDGE_LOOP ( 'NONE', ( #42200, #123672, #30524, #131031 ) ) ;
#66449=DIRECTION ( 'NONE',  ( 0.7071067811865487940, 0.7071067811865463515, -0.000000000000000000 ) ) ;
#66451=DIRECTION ( 'NONE',  ( -0.7071067811865487940, 0.7071067811865463515, -0.000000000000000000 ) ) ;
#66452=CARTESIAN_POINT ( 'NONE',  ( -6.299744871391586898, -27.71228299555210484, 4.000000000000000000 ) ) ;
#66453=DIRECTION ( 'NONE',  ( 0.6830127018922180770, -0.6830127018922204085, -0.2588190451025213501 ) ) ;
#66454=DIRECTION ( 'NONE',  ( -0.3543493200069162685, -0.000000000000000000, -0.9351131265310288487 ) ) ;
#66455=CARTESIAN_POINT ( 'NONE',  ( 0.000000000000000000, 0.000000000000000000, 5.000000000000000000 ) ) ;
#66456=ORIENTED_EDGE ( 'NONE', *, *, #130779, .T. ) ;
#66457=EDGE_CURVE ( 'NONE', #12864, #31545, #16787, .T. ) ;
#66460=VERTEX_POINT ( 'NONE', #88306 ) ;
#66461=EDGE_LOOP ( 'NONE', ( #111337, #55608, #45591, #103409 ) ) ;
#66462=EDGE_CURVE ( 'NONE', #90802, #49877, #95773, .T. ) ;
#66463=ADVANCED_FACE ( 'NONE', ( #106622 ), #71922, .F. ) ;
#66464=ORIENTED_EDGE ( 'NONE', *, *, #143484, .F. ) ;
#66466=VECTOR ( 'NONE', #117232, 1000.000000000000000 ) ;
#66467=ORIENTED_EDGE ( 'NONE', *, *, #30997, .T. ) ;
#66468=LINE ( 'NONE', #110632, #58301 ) ;
#66469=AXIS2_PLACEMENT_3D ( 'NONE', #16099, #71980, #94401 ) ;
#66472=CARTESIAN_POINT ( 'NONE',  ( 19.83957586139685247, 9.091547215995101183, 4.000000000000000000 ) ) ;
#66473=EDGE_CURVE ( 'NONE', #63744, #117579, #28394, .T. ) ;
#66474=ORIENTED_EDGE ( 'NONE', *, *, #24057, .F. ) ;
#66475=DIRECTION ( 'NONE',  ( 0.7071067811865487940, 0.7071067811865463515, 0.000000000000000000 ) ) ;
#66478=PLANE ( 'NONE',  #84131 ) ;
#66480=DIRECTION ( 'NONE',  ( -0.7071067811865486830, 0.7071067811865464625, 0.000000000000000000 ) ) ;
#66481=ORIENTED_EDGE ( 'NONE', *, *, #113676, .T. ) ;
#66482=DIRECTION ( 'NONE',  ( 0.7071067811865487940, 0.7071067811865463515, 0.000000000000000000 ) ) ;
#66483=VERTEX_POINT ( 'NONE', #84225 ) ;
#66485=ORIENTED_EDGE ( 'NONE', *, *, #87454, .F. ) ;
#66487=VECTOR ( 'NONE', #3717, 1000.000000000000000 ) ;
#66489=VECTOR ( 'NONE', #57902, 1000.000000000000000 ) ;
#66490=CARTESIAN_POINT ( 'NONE',  ( -10.39656807105350467, -14.24070752338413648, 19.24067776001723473 ) ) ;
#66492=PLANE ( 'NONE',  #44232 ) ;
#66493=VERTEX_POINT ( 'NONE', #54966 ) ;
#66494=EDGE_CURVE ( 'NONE', #134557, #116711, #62456, .T. ) ;
#66495=EDGE_CURVE ( 'NONE', #23600, #68847, #65869, .T. ) ;
#66497=DIRECTION ( 'NONE',  ( -0.6830127018922180770, -0.6830127018922204085, -0.2588190451025213501 ) ) ;
#66498=PLANE ( 'NONE',  #1978 ) ;
#66499=VECTOR ( 'NONE', #40759, 1000.000000000000000 ) ;
#66501=VERTEX_POINT ( 'NONE', #10692 ) ;
#66502=ORIENTED_EDGE ( 'NONE', *, *, #125759, .T. ) ;
#66503=ORIENTED_EDGE ( 'NONE', *, *, #97515, .T. ) ;
#66504=CARTESIAN_POINT ( 'NONE',  ( 1.171830600776463838, -11.24070752338416845, 4.000000000000000000 ) ) ;
#66505=LINE ( 'NONE', #123020, #104234 ) ;
#66508=DIRECTION ( 'NONE',  ( -0.000000000000000000, -0.3543493200069152693, 0.9351131265310292928 ) ) ;
#66509=CARTESIAN_POINT ( 'NONE',  ( -27.18398860626900060, 28.73617430169806042, 5.000000000000000000 ) ) ;
#66510=DIRECTION ( 'NONE',  ( -1.000000000000000000, 0.000000000000000000, 0.000000000000000000 ) ) ;
#66511=CARTESIAN_POINT ( 'NONE',  ( 69.18398860626899705, 28.73617430169835529, 5.000000000000000000 ) ) ;
#66512=DIRECTION ( 'NONE',  ( -0.3543493200069162685, -0.000000000000000000, -0.9351131265310288487 ) ) ;
#66514=DIRECTION ( 'NONE',  ( 0.7071067811865487940, 0.7071067811865463515, 0.000000000000000000 ) ) ;
#66515=ORIENTED_EDGE ( 'NONE', *, *, #124051, .F. ) ;
#66516=CARTESIAN_POINT ( 'NONE',  ( 3.792893218813432998, 6.759292476615651246, 5.000000000000000000 ) ) ;
#66517=ORIENTED_EDGE ( 'NONE', *, *, #7309, .F. ) ;
#66518=PLANE ( 'NONE',  #80738 ) ;
#66519=PLANE ( 'NONE',  #32559 ) ;
#66520=ORIENTED_EDGE ( 'NONE', *, *, #141747, .T. ) ;
#66521=VECTOR ( 'NONE', #108621, 1000.000000000000000 ) ;
#66522=DIRECTION ( 'NONE',  ( -0.7071067811865487940, 0.7071067811865463515, -0.000000000000000000 ) ) ;
#66523=ORIENTED_EDGE ( 'NONE', *, *, #17378, .T. ) ;
#66524=FACE_OUTER_BOUND ( 'NONE', #134282, .T. ) ;
#66525=ORIENTED_EDGE ( 'NONE', *, *, #58628, .T. ) ;
#66526=CARTESIAN_POINT ( 'NONE',  ( -44.99451991528749772, 28.92564299267969474, 4.000000000000000000 ) ) ;
#66529=AXIS2_PLACEMENT_3D ( 'NONE', #74630, #51449, #39138 ) ;
#66533=DIRECTION ( 'NONE',  ( 0.7071067811865486830, -0.7071067811865464625, -0.000000000000000000 ) ) ;
#66534=DIRECTION ( 'NONE',  ( 0.7071067811865487940, 0.7071067811865463515, 0.000000000000000000 ) ) ;
#66535=CARTESIAN_POINT ( 'NONE',  ( -35.99451991528749772, 28.92564299267963079, 4.000000000000000000 ) ) ;
#66536=LINE ( 'NONE', #11383, #50820 ) ;
#66539=VECTOR ( 'NONE', #136813, 1000.000000000000000 ) ;
#66540=FACE_OUTER_BOUND ( 'NONE', #1326, .T. ) ;
#66542=ORIENTED_EDGE ( 'NONE', *, *, #30562, .F. ) ;
#66543=ORIENTED_EDGE ( 'NONE', *, *, #111896, .F. ) ;
#66544=CARTESIAN_POINT ( 'NONE',  ( 45.18398860626900415, 28.73617430169818832, 5.000000000000000000 ) ) ;
#66545=ORIENTED_EDGE ( 'NONE', *, *, #35233, .T. ) ;
#66546=CARTESIAN_POINT ( 'NONE',  ( -18.18398860626898994, 28.73617430169800002, 5.000000000000000000 ) ) ;
#66547=LINE ( 'NONE', #110718, #27812 ) ;
#66549=ORIENTED_EDGE ( 'NONE', *, *, #17417, .T. ) ;
#66550=CARTESIAN_POINT ( 'NONE',  ( 17.67183060077634948, 14.25929247661557397, 4.000000000000000000 ) ) ;
#66551=LINE ( 'NONE', #131808, #118152 ) ;
#66554=LINE ( 'NONE', #14298, #28013 ) ;
#66555=CARTESIAN_POINT ( 'NONE',  ( 24.48921356237309510, -27.52281430457072631, 5.000000000000000000 ) ) ;
#66556=ADVANCED_FACE ( 'NONE', ( #78144 ), #14294, .T. ) ;
#66557=ADVANCED_FACE ( 'NONE', ( #57832 ), #35374, .F. ) ;
#66558=LINE ( 'NONE', #46999, #74957 ) ;
#66559=CARTESIAN_POINT ( 'NONE',  ( -7.828169399223478209, 18.75929247661553134, 4.000000000000000000 ) ) ;
#66560=ORIENTED_EDGE ( 'NONE', *, *, #109366, .T. ) ;
#66561=PLANE ( 'NONE',  #120653 ) ;
#66562=CARTESIAN_POINT ( 'NONE',  ( -33.18398860626899705, 28.73617430169810305, 5.000000000000000000 ) ) ;
#66563=CARTESIAN_POINT ( 'NONE',  ( 2.999999999999987121, -1.447814304570818500, 5.000000000000000000 ) ) ;
#66564=CARTESIAN_POINT ( 'NONE',  ( 36.18398860626899705, 28.73617430169812437, 5.000000000000000000 ) ) ;
#66565=CARTESIAN_POINT ( 'NONE',  ( -72.29974487139158157, -27.71228299555256669, 4.000000000000000000 ) ) ;
#66566=ADVANCED_FACE ( 'NONE', ( #45537 ), #36073, .F. ) ;
#66567=EDGE_CURVE ( 'NONE', #118822, #29420, #1463, .T. ) ;
#66569=EDGE_LOOP ( 'NONE', ( #21089, #52998, #86195, #16829 ) ) ;
#66573=ORIENTED_EDGE ( 'NONE', *, *, #128471, .T. ) ;
#66575=DIRECTION ( 'NONE',  ( -0.6830127018922181881, 0.6830127018922202975, -0.2588190451025214056 ) ) ;
#66576=LINE ( 'NONE', #121636, #91905 ) ;
#66578=CARTESIAN_POINT ( 'NONE',  ( -8.999999999999932498, -15.41253812416059787, 4.000000000000000000 ) ) ;
#66582=CARTESIAN_POINT ( 'NONE',  ( 32.20710678118632586, 9.759292476615621936, 5.000000000000000000 ) ) ;
#66585=ORIENTED_EDGE ( 'NONE', *, *, #131857, .T. ) ;
#66587=VECTOR ( 'NONE', #26068, 1000.000000000000000 ) ;
#66588=CARTESIAN_POINT ( 'NONE',  ( -30.79289321881324781, -20.24070752338407431, 5.000000000000000000 ) ) ;
#66589=EDGE_CURVE ( 'NONE', #141779, #43430, #23753, .T. ) ;
#66590=ORIENTED_EDGE ( 'NONE', *, *, #109095, .T. ) ;
#66591=ORIENTED_EDGE ( 'NONE', *, *, #93787, .F. ) ;
#66592=ORIENTED_EDGE ( 'NONE', *, *, #79086, .T. ) ;
#66593=CARTESIAN_POINT ( 'NONE',  ( -13.49999999999991118, 12.43112307739206024, 4.000000000000000000 ) ) ;
#66596=LINE ( 'NONE', #54313, #97400 ) ;
#66598=CARTESIAN_POINT ( 'NONE',  ( 63.18398860626900415, 28.73617430169831621, 5.000000000000000000 ) ) ;
#66599=LINE ( 'NONE', #110769, #46494 ) ;
#66600=CARTESIAN_POINT ( 'NONE',  ( -51.18398860626899705, 28.73617430169823095, 5.000000000000000000 ) ) ;
#66601=ORIENTED_EDGE ( 'NONE', *, *, #102841, .T. ) ;
#66602=VECTOR ( 'NONE', #60955, 1000.000000000000000 ) ;
#66603=ORIENTED_EDGE ( 'NONE', *, *, #67017, .F. ) ;
#66605=VERTEX_POINT ( 'NONE', #46991 ) ;
#66607=EDGE_CURVE ( 'NONE', #19355, #61417, #80298, .T. ) ;
#66608=ADVANCED_FACE ( 'NONE', ( #44840 ), #112201, .F. ) ;
#66609=LINE ( 'NONE', #19517, #130825 ) ;
#66611=CARTESIAN_POINT ( 'NONE',  ( 0.000000000000000000, 0.000000000000000000, 5.000000000000000000 ) ) ;
#66612=CARTESIAN_POINT ( 'NONE',  ( 12.18398860626900060, 28.73617430169795739, 5.000000000000000000 ) ) ;
#66613=ADVANCED_FACE ( 'NONE', ( #25160 ), #110719, .F. ) ;
#66614=CARTESIAN_POINT ( 'NONE',  ( -21.48921356237309155, -27.52281430457070499, 5.000000000000000000 ) ) ;
#66615=DIRECTION ( 'NONE',  ( -0.000000000000000000, 0.000000000000000000, 1.000000000000000000 ) ) ;
#66616=AXIS2_PLACEMENT_3D ( 'NONE', #124582, #25259, #122422 ) ;
#66617=VERTEX_POINT ( 'NONE', #123799 ) ;
#66618=EDGE_CURVE ( 'NONE', #102321, #13412, #69412, .T. ) ;
#66619=LINE ( 'NONE', #55033, #90383 ) ;
#66621=VERTEX_POINT ( 'NONE', #113598 ) ;
#66622=FACE_OUTER_BOUND ( 'NONE', #26959, .T. ) ;
#66623=ORIENTED_EDGE ( 'NONE', *, *, #13533, .T. ) ;
#66624=FACE_OUTER_BOUND ( 'NONE', #55961, .T. ) ;
#66626=LINE ( 'NONE', #10077, #101486 ) ;
#66628=EDGE_LOOP ( 'NONE', ( #799, #115772, #39022, #131058 ) ) ;
#66629=AXIS2_PLACEMENT_3D ( 'NONE', #37566, #36827, #137585 ) ;
#66630=ORIENTED_EDGE ( 'NONE', *, *, #86749, .T. ) ;
#66632=CARTESIAN_POINT ( 'NONE',  ( 0.000000000000000000, 0.000000000000000000, 5.000000000000000000 ) ) ;
#66634=CARTESIAN_POINT ( 'NONE',  ( 15.48921356237309510, -27.52281430457066236, 5.000000000000000000 ) ) ;
#66636=CARTESIAN_POINT ( 'NONE',  ( 13.49999999999990052, 16.18958161055404332, -11.56426086740808223 ) ) ;
#66637=EDGE_CURVE ( 'NONE', #93700, #99074, #89030, .T. ) ;
#66638=LINE ( 'NONE', #55053, #78362 ) ;
#66639=DIRECTION ( 'NONE',  ( -0.7071067811865486830, -0.7071067811865464625, -0.000000000000000000 ) ) ;
#66640=CARTESIAN_POINT ( 'NONE',  ( -9.707013264292978505, -21.74070752338405654, 4.999753212805220670 ) ) ;
#66642=ORIENTED_EDGE ( 'NONE', *, *, #22790, .T. ) ;
#66643=FACE_OUTER_BOUND ( 'NONE', #1994, .T. ) ;
#66644=EDGE_CURVE ( 'NONE', #2187, #106533, #55681, .T. ) ;
#66645=LINE ( 'NONE', #121002, #68077 ) ;
#66646=VERTEX_POINT ( 'NONE', #51227 ) ;
#66648=ORIENTED_EDGE ( 'NONE', *, *, #45372, .F. ) ;
#66649=DIRECTION ( 'NONE',  ( 0.7071067811865487940, 0.7071067811865463515, 0.000000000000000000 ) ) ;
#66650=ORIENTED_EDGE ( 'NONE', *, *, #44549, .T. ) ;
#66654=DIRECTION ( 'NONE',  ( -0.7071067811865486830, -0.7071067811865464625, 0.000000000000000000 ) ) ;
#66655=EDGE_CURVE ( 'NONE', #88422, #93029, #26479, .T. ) ;
#66656=DIRECTION ( 'NONE',  ( -0.7071067811865486830, -0.7071067811865464625, 0.000000000000000000 ) ) ;
#66657=DIRECTION ( 'NONE',  ( -0.7071067811865486830, 0.7071067811865464625, 0.000000000000000000 ) ) ;
#66658=ADVANCED_FACE ( 'NONE', ( #14995 ), #92544, .F. ) ;
#66659=VERTEX_POINT ( 'NONE', #37498 ) ;
#66660=VECTOR ( 'NONE', #141322, 1000.000000000000000 ) ;
#66661=CARTESIAN_POINT ( 'NONE',  ( 51.18398860626899705, 28.73617430169823095, 5.000000000000000000 ) ) ;
#66662=ORIENTED_EDGE ( 'NONE', *, *, #39052, .F. ) ;
#66663=CARTESIAN_POINT ( 'NONE',  ( -10.82816939922344979, -17.24070752338410628, 4.000000000000000000 ) ) ;
#66664=EDGE_CURVE ( 'NONE', #109399, #20187, #49093, .T. ) ;
#66666=ORIENTED_EDGE ( 'NONE', *, *, #58843, .T. ) ;
#66668=( BOUNDED_CURVE ( )  B_SPLINE_CURVE ( 3, ( #58026, #125394, #48539, #5712 ),
 .UNSPECIFIED., .F., .T. ) 
 B_SPLINE_CURVE_WITH_KNOTS ( ( 4, 4 ),
 ( 5.005968288816736944, 5.074607125596340751 ),
 .UNSPECIFIED. ) 
 CURVE ( )  GEOMETRIC_REPRESENTATION_ITEM ( )  RATIONAL_B_SPLINE_CURVE ( ( 1.000000000000000000, 0.9996074310407765395, 0.9996074310407765395, 1.000000000000000000 ) ) 
 REPRESENTATION_ITEM ( '' )  );
#66669=CARTESIAN_POINT ( 'NONE',  ( -3.792893218813431222, 3.759292476615678336, 5.000000000000000000 ) ) ;
#66670=CARTESIAN_POINT ( 'NONE',  ( 0.3281693992235323876, -6.740707523384212863, 4.000000000000000000 ) ) ;
#66671=ORIENTED_EDGE ( 'NONE', *, *, #101707, .T. ) ;
#66672=ORIENTED_EDGE ( 'NONE', *, *, #26359, .F. ) ;
#66673=VERTEX_POINT ( 'NONE', #81734 ) ;
#66674=PLANE ( 'NONE',  #98225 ) ;
#66676=CARTESIAN_POINT ( 'NONE',  ( 34.75611968250419181, -1.294349301475941072, 4.955485411084880276 ) ) ;
#66678=DIRECTION ( 'NONE',  ( -0.7071067811865487940, 0.7071067811865463515, 0.000000000000000000 ) ) ;
#66679=DIRECTION ( 'NONE',  ( -0.6830127018922181881, 0.6830127018922202975, -0.2588190451025214056 ) ) ;
#66680=ORIENTED_EDGE ( 'NONE', *, *, #108355, .F. ) ;
#66682=EDGE_CURVE ( 'NONE', #72725, #17934, #59271, .T. ) ;
#66683=CARTESIAN_POINT ( 'NONE',  ( 0.08314806772930470602, 21.75929247661549581, 7.311836541448051285 ) ) ;
#66684=DIRECTION ( 'NONE',  ( 0.7071067811865487940, 0.7071067811865463515, 0.000000000000000000 ) ) ;
#66686=CARTESIAN_POINT ( 'NONE',  ( -14.99999999999989164, -6.412538124160687580, 4.000000000000000000 ) ) ;
#66687=PLANE ( 'NONE',  #16905 ) ;
#66689=DIRECTION ( 'NONE',  ( 0.3543493200069162685, -0.000000000000000000, -0.9351131265310288487 ) ) ;
#66690=VERTEX_POINT ( 'NONE', #59962 ) ;
#66691=EDGE_LOOP ( 'NONE', ( #75380, #137846, #142545, #36201 ) ) ;
#66692=EDGE_CURVE ( 'NONE', #83448, #94185, #72302, .T. ) ;
#66693=DIRECTION ( 'NONE',  ( -0.7071067811865486830, -0.7071067811865464625, -0.000000000000000000 ) ) ;
#66694=DIRECTION ( 'NONE',  ( 0.7071067811865487940, 0.7071067811865463515, 0.000000000000000000 ) ) ;
#66695=ORIENTED_EDGE ( 'NONE', *, *, #53833, .F. ) ;
#66696=CARTESIAN_POINT ( 'NONE',  ( 63.48921356237309510, -27.52281430457099631, 5.000000000000000000 ) ) ;
#66697=LINE ( 'NONE', #11556, #46267 ) ;
#66698=VECTOR ( 'NONE', #19187, 1000.000000000000000 ) ;
#66699=CARTESIAN_POINT ( 'NONE',  ( 4.171830600776447184, -2.240707523384257716, 4.000000000000000000 ) ) ;
#66700=LINE ( 'NONE', #12300, #55903 ) ;
#66701=DIRECTION ( 'NONE',  ( 0.6830127018922180770, -0.6830127018922204085, -0.2588190451025213501 ) ) ;
#66702=PLANE ( 'NONE',  #114302 ) ;
#66703=LINE ( 'NONE', #122482, #8947 ) ;
#66705=FACE_OUTER_BOUND ( 'NONE', #107748, .T. ) ;
#66706=FACE_OUTER_BOUND ( 'NONE', #24472, .T. ) ;
#66707=LINE ( 'NONE', #97907, #122932 ) ;
#66708=DIRECTION ( 'NONE',  ( 0.7071067811865487940, 0.7071067811865463515, 0.000000000000000000 ) ) ;
#66709=EDGE_LOOP ( 'NONE', ( #58436, #98578, #32233, #20003 ) ) ;
#66713=EDGE_LOOP ( 'NONE', ( #88545, #101789, #117560, #101197 ) ) ;
#66714=ORIENTED_EDGE ( 'NONE', *, *, #7999, .T. ) ;
#66715=LINE ( 'NONE', #123259, #103485 ) ;
#66716=DIRECTION ( 'NONE',  ( -0.3543493200069163240, 0.000000000000000000, -0.9351131265310288487 ) ) ;
#66718=AXIS2_PLACEMENT_3D ( 'NONE', #79540, #36676, #46176 ) ;
#66719=FACE_OUTER_BOUND ( 'NONE', #25067, .T. ) ;
#66723=FACE_OUTER_BOUND ( 'NONE', #21322, .T. ) ;
#66725=EDGE_CURVE ( 'NONE', #80548, #77764, #61424, .T. ) ;
#66726=EDGE_CURVE ( 'NONE', #70409, #123460, #80998, .T. ) ;
#66727=CARTESIAN_POINT ( 'NONE',  ( 20.21837311707492191, 21.74787736706807095, 4.999607392498048419 ) ) ;
#66728=DIRECTION ( 'NONE',  ( -0.000000000000000000, 1.000000000000000000, -0.000000000000000000 ) ) ;
#66729=DIRECTION ( 'NONE',  ( 0.7071067811865486830, -0.7071067811865464625, -0.000000000000000000 ) ) ;
#66732=CARTESIAN_POINT ( 'NONE',  ( -11.81601139373100651, 28.73617430169779041, 5.000000000000000000 ) ) ;
#66733=CARTESIAN_POINT ( 'NONE',  ( 12.32816939922343913, -18.74070752338409562, 4.000000000000000000 ) ) ;
#66734=VECTOR ( 'NONE', #31149, 1000.000000000000000 ) ;
#66736=DIRECTION ( 'NONE',  ( 0.7071067811865486830, 0.7071067811865464625, 0.000000000000000000 ) ) ;
#66737=EDGE_CURVE ( 'NONE', #120060, #134557, #25889, .T. ) ;
#66738=EDGE_CURVE ( 'NONE', #57857, #122903, #27296, .T. ) ;
#66739=VERTEX_POINT ( 'NONE', #136787 ) ;
#66740=ORIENTED_EDGE ( 'NONE', *, *, #120773, .F. ) ;
#66742=EDGE_CURVE ( 'NONE', #88957, #46507, #71550, .T. ) ;
#66745=CARTESIAN_POINT ( 'NONE',  ( -54.18398860626899705, 28.73617430169825226, 5.000000000000000000 ) ) ;
#66746=EDGE_CURVE ( 'NONE', #43903, #57318, #17835, .T. ) ;
#66747=CARTESIAN_POINT ( 'NONE',  ( 26.99999999999980815, 16.55218569542899587, 5.000000000000000000 ) ) ;
#66749=CARTESIAN_POINT ( 'NONE',  ( -9.989119713460445027, -22.02621442084248216, 4.990779571109223767 ) ) ;
#66750=ADVANCED_FACE ( 'NONE', ( #50503 ), #93987, .F. ) ;
#66752=ORIENTED_EDGE ( 'NONE', *, *, #102751, .F. ) ;
#66753=ORIENTED_EDGE ( 'NONE', *, *, #52470, .F. ) ;
#66754=DIRECTION ( 'NONE',  ( -0.000000000000000000, 0.3543493200069153248, 0.9351131265310292928 ) ) ;
#66755=VECTOR ( 'NONE', #6376, 1000.000000000000000 ) ;
#66756=PLANE ( 'NONE',  #1497 ) ;
#66757=VECTOR ( 'NONE', #53281, 1000.000000000000000 ) ;
#66758=EDGE_CURVE ( 'NONE', #133870, #4434, #138948, .T. ) ;
#66759=ORIENTED_EDGE ( 'NONE', *, *, #839, .F. ) ;
#66760=ORIENTED_EDGE ( 'NONE', *, *, #44490, .F. ) ;
#66762=ORIENTED_EDGE ( 'NONE', *, *, #123761, .T. ) ;
#66763=DIRECTION ( 'NONE',  ( -1.000000000000000000, 0.000000000000000000, 0.000000000000000000 ) ) ;
#66764=CARTESIAN_POINT ( 'NONE',  ( -34.92500000000001137, -12.18334561358944335, 4.500000000000000888 ) ) ;
#66765=DIRECTION ( 'NONE',  ( -0.7071067811865486830, -0.7071067811865464625, 0.000000000000000000 ) ) ;
#66766=EDGE_CURVE ( 'NONE', #92427, #69962, #116469, .T. ) ;
#66769=CARTESIAN_POINT ( 'NONE',  ( 12.48921356237309155, -27.52281430457064104, 5.000000000000000000 ) ) ;
#66771=ORIENTED_EDGE ( 'NONE', *, *, #40962, .T. ) ;
#66773=ORIENTED_EDGE ( 'NONE', *, *, #140904, .T. ) ;
#66775=DIRECTION ( 'NONE',  ( 0.6830127018922181881, 0.6830127018922202975, -0.2588190451025214056 ) ) ;
#66776=FACE_OUTER_BOUND ( 'NONE', #9536, .T. ) ;
#66777=VERTEX_POINT ( 'NONE', #128081 ) ;
#66778=DIRECTION ( 'NONE',  ( 0.7071067811865487940, 0.7071067811865463515, 0.000000000000000000 ) ) ;
#66779=EDGE_CURVE ( 'NONE', #81042, #96318, #73008, .T. ) ;
#66780=FACE_OUTER_BOUND ( 'NONE', #74685, .T. ) ;
#66781=CARTESIAN_POINT ( 'NONE',  ( -28.06996025486391133, -0.7407075233842701500, 13.87443053587617747 ) ) ;
#66783=LINE ( 'NONE', #1481, #49045 ) ;
#66784=FACE_BOUND ( 'NONE', #92743, .T. ) ;
#66785=VERTEX_POINT ( 'NONE', #19990 ) ;
#66786=CARTESIAN_POINT ( 'NONE',  ( -12.18398860626900060, 28.73617430169795739, 5.000000000000000000 ) ) ;
#66787=DIRECTION ( 'NONE',  ( -0.000000000000000000, 0.000000000000000000, -1.000000000000000000 ) ) ;
#66788=VERTEX_POINT ( 'NONE', #85249 ) ;
#66789=DIRECTION ( 'NONE',  ( 0.000000000000000000, 0.000000000000000000, -1.000000000000000000 ) ) ;
#66790=ORIENTED_EDGE ( 'NONE', *, *, #57757, .T. ) ;
#66791=ORIENTED_EDGE ( 'NONE', *, *, #105935, .T. ) ;
#66792=DIRECTION ( 'NONE',  ( 0.7071067811865487940, -0.7071067811865463515, 0.000000000000000000 ) ) ;
#66793=EDGE_CURVE ( 'NONE', #77659, #130555, #97558, .T. ) ;
#66794=EDGE_LOOP ( 'NONE', ( #100273, #66826, #93211, #34109 ) ) ;
#66796=ORIENTED_EDGE ( 'NONE', *, *, #92697, .F. ) ;
#66797=DIRECTION ( 'NONE',  ( -0.000000000000000000, -0.3543493200069152693, 0.9351131265310292928 ) ) ;
#66798=CARTESIAN_POINT ( 'NONE',  ( -3.707106781186507938, -18.74070752338409207, 5.000000000000000000 ) ) ;
#66800=DIRECTION ( 'NONE',  ( -0.7071067811865487940, 0.7071067811865463515, -0.000000000000000000 ) ) ;
#66801=ORIENTED_EDGE ( 'NONE', *, *, #2875, .T. ) ;
#66805=DIRECTION ( 'NONE',  ( 0.7071067811865487940, -0.7071067811865463515, 0.000000000000000000 ) ) ;
#66806=PLANE ( 'NONE',  #1877 ) ;
#66807=EDGE_CURVE ( 'NONE', #139229, #96774, #62828, .T. ) ;
#66808=CARTESIAN_POINT ( 'NONE',  ( -34.92500000000001137, 22.22500000000000142, 4.500000000000000888 ) ) ;
#66810=ORIENTED_EDGE ( 'NONE', *, *, #83919, .F. ) ;
#66811=ORIENTED_EDGE ( 'NONE', *, *, #132864, .T. ) ;
#66812=ORIENTED_EDGE ( 'NONE', *, *, #120840, .T. ) ;
#66813=FACE_OUTER_BOUND ( 'NONE', #49635, .T. ) ;
#66814=AXIS2_PLACEMENT_3D ( 'NONE', #51993, #9137, #96174 ) ;
#66815=VECTOR ( 'NONE', #52205, 1000.000000000000000 ) ;
#66816=DIRECTION ( 'NONE',  ( -0.7071067811865486830, 0.7071067811865464625, 0.000000000000000000 ) ) ;
#66817=VERTEX_POINT ( 'NONE', #109155 ) ;
#66818=AXIS2_PLACEMENT_3D ( 'NONE', #79115, #68248, #69658 ) ;
#66819=AXIS2_PLACEMENT_3D ( 'NONE', #121838, #34157, #134924 ) ;
#66820=VERTEX_POINT ( 'NONE', #40366 ) ;
#66821=DIRECTION ( 'NONE',  ( 0.7071067811865486830, -0.7071067811865463515, 0.000000000000000000 ) ) ;
#66822=EDGE_CURVE ( 'NONE', #123220, #23205, #42508, .T. ) ;
#66823=VECTOR ( 'NONE', #112155, 1000.000000000000000 ) ;
#66824=ADVANCED_FACE ( 'NONE', ( #142521 ), #96124, .T. ) ;
#66825=LINE ( 'NONE', #123366, #106390 ) ;
#66826=ORIENTED_EDGE ( 'NONE', *, *, #114687, .F. ) ;
#66827=CARTESIAN_POINT ( 'NONE',  ( -0.1561230773924060511, -22.22499999999999787, 4.000000000000000000 ) ) ;
#66828=VECTOR ( 'NONE', #25418, 1000.000000000000000 ) ;
#66829=AXIS2_PLACEMENT_3D ( 'NONE', #36582, #91684, #92373 ) ;
#66830=CARTESIAN_POINT ( 'NONE',  ( 14.70025512860841133, -27.71228299555195917, 4.000000000000000000 ) ) ;
#66831=EDGE_CURVE ( 'NONE', #62699, #50020, #74411, .T. ) ;
#66833=DIRECTION ( 'NONE',  ( -0.6830127018922181881, 0.6830127018922202975, -0.2588190451025214056 ) ) ;
#66834=ORIENTED_EDGE ( 'NONE', *, *, #79496, .T. ) ;
#66836=CARTESIAN_POINT ( 'NONE',  ( 20.70025512860841133, -27.71228299555191654, 4.000000000000000000 ) ) ;
#66837=LINE ( 'NONE', #142956, #109774 ) ;
#66838=CYLINDRICAL_SURFACE ( 'NONE', #10095, 0.5000000000000004441 ) ;
#66839=ORIENTED_EDGE ( 'NONE', *, *, #48955, .F. ) ;
#66841=FACE_OUTER_BOUND ( 'NONE', #44137, .T. ) ;
#66843=CARTESIAN_POINT ( 'NONE',  ( 20.99999999999986855, 17.96639925780208458, 5.000000000000000000 ) ) ;
#66844=FACE_OUTER_BOUND ( 'NONE', #52713, .T. ) ;
#66845=CARTESIAN_POINT ( 'NONE',  ( 33.18398860626899705, 28.73617430169810305, 5.000000000000000000 ) ) ;
#66846=EDGE_LOOP ( 'NONE', ( #46745, #3411, #124492, #23049 ) ) ;
#66847=EDGE_CURVE ( 'NONE', #33404, #128631, #107007, .T. ) ;
#66848=CARTESIAN_POINT ( 'NONE',  ( -34.49999999999976552, -2.945670655169033481, 4.994342998332163219 ) ) ;
#66849=ADVANCED_FACE ( 'NONE', ( #9081 ), #8376, .T. ) ;
#66850=DIRECTION ( 'NONE',  ( 1.000000000000000000, 0.000000000000000000, 0.000000000000000000 ) ) ;
#66851=DIRECTION ( 'NONE',  ( 0.7071067811865487940, -0.7071067811865463515, 0.000000000000000000 ) ) ;
#66852=VERTEX_POINT ( 'NONE', #52624 ) ;
#66853=VECTOR ( 'NONE', #33400, 1000.000000000000000 ) ;
#66854=CARTESIAN_POINT ( 'NONE',  ( 10.49999999999993960, 16.08746187583908593, 4.000000000000000000 ) ) ;
#66855=VECTOR ( 'NONE', #95788, 1000.000000000000000 ) ;
#66856=PLANE ( 'NONE',  #116350 ) ;
#66857=AXIS2_PLACEMENT_3D ( 'NONE', #136039, #103390, #36724 ) ;
#66860=PLANE ( 'NONE',  #55396 ) ;
#66862=ORIENTED_EDGE ( 'NONE', *, *, #40914, .F. ) ;
#66863=EDGE_CURVE ( 'NONE', #65778, #85291, #75138, .T. ) ;
#66866=AXIS2_PLACEMENT_3D ( 'NONE', #86323, #110178, #142830 ) ;
#66867=ORIENTED_EDGE ( 'NONE', *, *, #64449, .F. ) ;
#66868=VECTOR ( 'NONE', #81652, 1000.000000000000000 ) ;
#66869=CARTESIAN_POINT ( 'NONE',  ( 30.18398860626900060, 28.73617430169808173, 5.000000000000000000 ) ) ;
#66870=CARTESIAN_POINT ( 'NONE',  ( -4.499999999999962697, 10.46639925780215563, 5.000000000000000000 ) ) ;
#66871=ORIENTED_EDGE ( 'NONE', *, *, #107950, .F. ) ;
#66872=CARTESIAN_POINT ( 'NONE',  ( 31.49999999999977973, 13.56627193232217188, -10.57019076586061423 ) ) ;
#66873=DIRECTION ( 'NONE',  ( -0.000000000000000000, 0.3543493200069153248, 0.9351131265310292928 ) ) ;
#66876=CARTESIAN_POINT ( 'NONE',  ( -20.99999999999984723, -21.84840872380826582, 2.849755605029559380 ) ) ;
#66879=ORIENTED_EDGE ( 'NONE', *, *, #121692, .F. ) ;
#66880=VERTEX_POINT ( 'NONE', #141061 ) ;
#66881=LINE ( 'NONE', #45861, #32723 ) ;
#66882=ORIENTED_EDGE ( 'NONE', *, *, #39790, .T. ) ;
#66883=EDGE_LOOP ( 'NONE', ( #101663, #83664, #67040, #105780 ) ) ;
#66884=CARTESIAN_POINT ( 'NONE',  ( -72.48921356237309510, -27.52281430457106026, 5.000000000000000000 ) ) ;
#66885=CARTESIAN_POINT ( 'NONE',  ( -8.588385094051634638, 22.22500000000000497, 4.777194822843819466 ) ) ;
#66886=ORIENTED_EDGE ( 'NONE', *, *, #16096, .F. ) ;
#66888=CARTESIAN_POINT ( 'NONE',  ( 34.92499999999998295, -11.33753812416086504, 4.000000000000000000 ) ) ;
#66889=DIRECTION ( 'NONE',  ( -0.000000000000000000, 0.000000000000000000, 1.000000000000000000 ) ) ;
#66890=FACE_OUTER_BOUND ( 'NONE', #36633, .T. ) ;
#66892=ORIENTED_EDGE ( 'NONE', *, *, #82787, .T. ) ;
#66893=DIRECTION ( 'NONE',  ( 0.3543493200069163795, -9.265275131829747941E-33, -0.9351131265310288487 ) ) ;
#66894=CARTESIAN_POINT ( 'NONE',  ( -7.499999999999944045, -17.56887692260763245, 4.000000000000000000 ) ) ;
#66895=DIRECTION ( 'NONE',  ( 1.000000000000000000, 0.000000000000000000, 0.000000000000000000 ) ) ;
#66896=DIRECTION ( 'NONE',  ( 0.6830127018922180770, -0.6830127018922204085, -0.2588190451025213501 ) ) ;
#66897=CARTESIAN_POINT ( 'NONE',  ( -15.48921356237309510, -27.52281430457066236, 5.000000000000000000 ) ) ;
#66898=CARTESIAN_POINT ( 'NONE',  ( -18.48921356237309510, -27.52281430457068367, 5.000000000000000000 ) ) ;
#66899=PLANE ( 'NONE',  #105893 ) ;
#66901=CARTESIAN_POINT ( 'NONE',  ( 0.005480084712502889671, 28.92564299267938210, 4.000000000000000000 ) ) ;
#66902=EDGE_CURVE ( 'NONE', #123251, #119070, #41766, .T. ) ;
#66903=DIRECTION ( 'NONE',  ( -0.7071067811865487940, 0.7071067811865463515, 0.000000000000000000 ) ) ;
#66904=EDGE_LOOP ( 'NONE', ( #87635, #125862, #111334, #56460 ) ) ;
#66905=ORIENTED_EDGE ( 'NONE', *, *, #64644, .T. ) ;
#66907=EDGE_CURVE ( 'NONE', #125640, #22650, #130215, .T. ) ;
#66908=CARTESIAN_POINT ( 'NONE',  ( 0.000000000000000000, 0.000000000000000000, 5.000000000000000000 ) ) ;
#66909=ADVANCED_FACE ( 'NONE', ( #53341 ), #29442, .F. ) ;
#66910=DIRECTION ( 'NONE',  ( 0.7071067811865486830, -0.7071067811865464625, -0.000000000000000000 ) ) ;
#66911=ORIENTED_EDGE ( 'NONE', *, *, #112576, .T. ) ;
#66912=EDGE_CURVE ( 'NONE', #139562, #58036, #20709, .T. ) ;
#66917=EDGE_CURVE ( 'NONE', #36381, #117254, #5286, .T. ) ;
#66918=CARTESIAN_POINT ( 'NONE',  ( 32.48334561358932149, 22.22500000000000142, 4.500000000000000888 ) ) ;
#66919=ORIENTED_EDGE ( 'NONE', *, *, #121442, .F. ) ;
#66920=ORIENTED_EDGE ( 'NONE', *, *, #85066, .T. ) ;
#66921=CARTESIAN_POINT ( 'NONE',  ( 9.299744871391588674, -27.71228299555212971, 4.000000000000000000 ) ) ;
#66922=AXIS2_PLACEMENT_3D ( 'NONE', #19184, #30043, #7571 ) ;
#66923=AXIS2_PLACEMENT_3D ( 'NONE', #27241, #61369, #27977 ) ;
#66926=EDGE_CURVE ( 'NONE', #136439, #4199, #5984, .T. ) ;
#66927=CARTESIAN_POINT ( 'NONE',  ( -14.85700540165867345, 7.427722529079425762, 4.951096321256158284 ) ) ;
#66928=ORIENTED_EDGE ( 'NONE', *, *, #86789, .F. ) ;
#66929=EDGE_CURVE ( 'NONE', #11288, #49817, #71305, .T. ) ;
#66930=LINE ( 'NONE', #35766, #125201 ) ;
#66931=EDGE_LOOP ( 'NONE', ( #53705, #75899, #139573, #14353, #43360 ) ) ;
#66933=DIRECTION ( 'NONE',  ( 1.000000000000000000, 0.000000000000000000, 0.000000000000000000 ) ) ;
#66935=DIRECTION ( 'NONE',  ( 0.6830127018922180770, -0.6830127018922204085, -0.2588190451025213501 ) ) ;
#66936=DIRECTION ( 'NONE',  ( 0.7071067811865487940, 0.7071067811865463515, -0.000000000000000000 ) ) ;
#66937=EDGE_CURVE ( 'NONE', #2809, #874, #73441, .T. ) ;
#66939=LINE ( 'NONE', #122735, #3630 ) ;
#66941=DIRECTION ( 'NONE',  ( 0.6830127018922180770, -0.6830127018922204085, -0.2588190451025213501 ) ) ;
#66942=CARTESIAN_POINT ( 'NONE',  ( 63.29974487139158867, -27.71228299555250274, 4.000000000000000000 ) ) ;
#66943=DIRECTION ( 'NONE',  ( 1.000000000000000000, 0.000000000000000000, 0.000000000000000000 ) ) ;
#66944=VERTEX_POINT ( 'NONE', #95165 ) ;
#66946=DIRECTION ( 'NONE',  ( -0.6830127018922180770, -0.6830127018922204085, -0.2588190451025213501 ) ) ;
#66949=( BOUNDED_CURVE ( )  B_SPLINE_CURVE ( 3, ( #130765, #31432, #75654, #21259 ),
 .UNSPECIFIED., .F., .F. ) 
 B_SPLINE_CURVE_WITH_KNOTS ( ( 4, 4 ),
 ( 4.130769849943813909, 4.183600770845220751 ),
 .UNSPECIFIED. ) 
 CURVE ( )  GEOMETRIC_REPRESENTATION_ITEM ( )  RATIONAL_B_SPLINE_CURVE ( ( 1.000000000000000000, 0.9997674213408587196, 0.9997674213408587196, 1.000000000000000000 ) ) 
 REPRESENTATION_ITEM ( '' )  );
#66950=VECTOR ( 'NONE', #137163, 1000.000000000000000 ) ;
#66951=CARTESIAN_POINT ( 'NONE',  ( 60.18398860626900415, 28.73617430169829490, 5.000000000000000000 ) ) ;
#66953=CARTESIAN_POINT ( 'NONE',  ( 48.18398860626899705, 28.73617430169820608, 5.000000000000000000 ) ) ;
#66954=FACE_OUTER_BOUND ( 'NONE', #64026, .T. ) ;
#66955=ADVANCED_FACE ( 'NONE', ( #61862 ), #17594, .F. ) ;
#66956=FACE_OUTER_BOUND ( 'NONE', #87772, .T. ) ;
#66959=VECTOR ( 'NONE', #138919, 1000.000000000000000 ) ;
#66961=VECTOR ( 'NONE', #82389, 1000.000000000000227 ) ;
#66962=FACE_BOUND ( 'NONE', #69486, .T. ) ;
#66963=DIRECTION ( 'NONE',  ( -0.7071067811865486830, -0.7071067811865464625, 0.000000000000000000 ) ) ;
#66964=CARTESIAN_POINT ( 'NONE',  ( -1.499999999999984013, -11.94781430457070215, 5.000000000000000000 ) ) ;
#66965=CARTESIAN_POINT ( 'NONE',  ( -23.99999999999983302, -0.2811185226894510891, -5.995736974527457797 ) ) ;
#66967=ORIENTED_EDGE ( 'NONE', *, *, #91179, .T. ) ;
#66968=VECTOR ( 'NONE', #76719, 1000.000000000000000 ) ;
#66969=VECTOR ( 'NONE', #38132, 1000.000000000000000 ) ;
#66970=CARTESIAN_POINT ( 'NONE',  ( 5.816011393731002066, 28.73617430169783304, 5.000000000000000000 ) ) ;
#66971=ADVANCED_FACE ( 'NONE', ( #127829 ), #137983, .F. ) ;
#66972=ORIENTED_EDGE ( 'NONE', *, *, #79801, .F. ) ;
#66973=EDGE_LOOP ( 'NONE', ( #81415, #104461, #28754, #60082 ) ) ;
#66975=ORIENTED_EDGE ( 'NONE', *, *, #129421, .T. ) ;
#66976=CARTESIAN_POINT ( 'NONE',  ( -7.499999999999951150, 10.94296225409025958, -9.576120664313274133 ) ) ;
#66978=EDGE_CURVE ( 'NONE', #118739, #112217, #50969, .T. ) ;
#66979=ORIENTED_EDGE ( 'NONE', *, *, #121909, .F. ) ;
#66980=CARTESIAN_POINT ( 'NONE',  ( 18.48921356237309510, -27.52281430457068367, 5.000000000000000000 ) ) ;
#66982=PLANE ( 'NONE',  #26390 ) ;
#66983=CARTESIAN_POINT ( 'NONE',  ( -60.18398860626900415, 28.73617430169829490, 5.000000000000000000 ) ) ;
#66985=CARTESIAN_POINT ( 'NONE',  ( -14.20710678118643955, -11.24070752338416845, 5.000000000000000000 ) ) ;
#66986=CARTESIAN_POINT ( 'NONE',  ( 28.58990935480150952, 9.759292476615618384, 11.28811694763785489 ) ) ;
#66989=DIRECTION ( 'NONE',  ( -0.7071067811865486830, -0.7071067811865464625, 0.000000000000000000 ) ) ;
#66990=ORIENTED_EDGE ( 'NONE', *, *, #112961, .T. ) ;
#66992=CARTESIAN_POINT ( 'NONE',  ( 33.18398860626899705, 28.73617430169810305, 5.000000000000000000 ) ) ;
#66993=DIRECTION ( 'NONE',  ( 0.7071067811865487940, 0.7071067811865463515, -0.000000000000000000 ) ) ;
#66996=EDGE_LOOP ( 'NONE', ( #62659, #32642, #47356, #133998 ) ) ;
#66997=ADVANCED_FACE ( 'NONE', ( #7429 ), #15433, .T. ) ;
#67000=CARTESIAN_POINT ( 'NONE',  ( 11.51078643762690490, -27.52281430457047406, 5.000000000000000000 ) ) ;
#67001=DIRECTION ( 'NONE',  ( 0.7071067811865487940, 0.7071067811865463515, 0.000000000000000000 ) ) ;
#67003=CARTESIAN_POINT ( 'NONE',  ( -4.499999999999968914, 5.696342897626497148, -7.587980461218407413 ) ) ;
#67005=DIRECTION ( 'NONE',  ( -0.7071067811865486830, -0.7071067811865464625, -0.000000000000000000 ) ) ;
#67006=LINE ( 'NONE', #44578, #67342 ) ;
#67007=FACE_OUTER_BOUND ( 'NONE', #112515, .T. ) ;
#67008=CARTESIAN_POINT ( 'NONE',  ( 15.32816939922342847, -6.740707523384209310, 4.000000000000000000 ) ) ;
#67009=EDGE_LOOP ( 'NONE', ( #81254, #136289, #109295, #54203 ) ) ;
#67011=CARTESIAN_POINT ( 'NONE',  ( 15.00548008471250228, 28.92564299267927552, 4.000000000000000000 ) ) ;
#67012=CARTESIAN_POINT ( 'NONE',  ( 34.92499999999998295, 21.72500000000000142, 0.4999999999999995559 ) ) ;
#67013=DIRECTION ( 'NONE',  ( 0.3543493200069163240, -0.000000000000000000, 0.9351131265310288487 ) ) ;
#67014=ORIENTED_EDGE ( 'NONE', *, *, #10589, .T. ) ;
#67015=CARTESIAN_POINT ( 'NONE',  ( 16.49999999999988631, 22.01701374228156993, 2.453858888625593426 ) ) ;
#67016=CARTESIAN_POINT ( 'NONE',  ( -8.816011393731004731, 28.73617430169781173, 5.000000000000000000 ) ) ;
#67017=EDGE_CURVE ( 'NONE', #2775, #19628, #27774, .T. ) ;
#67020=DIRECTION ( 'NONE',  ( -0.7071067811865487940, 0.7071067811865463515, 0.000000000000000000 ) ) ;
#67021=VECTOR ( 'NONE', #82182, 1000.000000000000227 ) ;
#67023=AXIS2_PLACEMENT_3D ( 'NONE', #84081, #50708, #85448 ) ;
#67025=DIRECTION ( 'NONE',  ( -0.7071067811865486830, -0.7071067811865464625, -0.000000000000000000 ) ) ;
#67027=VECTOR ( 'NONE', #94750, 1000.000000000000000 ) ;
#67028=DIRECTION ( 'NONE',  ( -0.7071067811865487940, 0.7071067811865463515, 0.000000000000000000 ) ) ;
#67030=LINE ( 'NONE', #58345, #22853 ) ;
#67031=ORIENTED_EDGE ( 'NONE', *, *, #42439, .F. ) ;
#67032=EDGE_CURVE ( 'NONE', #86149, #90697, #127082, .T. ) ;
#67033=LINE ( 'NONE', #86655, #42050 ) ;
#67034=VERTEX_POINT ( 'NONE', #16908 ) ;
#67036=VECTOR ( 'NONE', #118746, 1000.000000000000000 ) ;
#67037=LINE ( 'NONE', #111220, #109575 ) ;
#67038=FACE_OUTER_BOUND ( 'NONE', #36973, .T. ) ;
#67039=CARTESIAN_POINT ( 'NONE',  ( -3.316579611327873600, -6.740707523384216415, 11.88629033278125036 ) ) ;
#67040=ORIENTED_EDGE ( 'NONE', *, *, #115004, .T. ) ;
#67041=VECTOR ( 'NONE', #48132, 1000.000000000000000 ) ;
#67042=LINE ( 'NONE', #35145, #140985 ) ;
#67043=CARTESIAN_POINT ( 'NONE',  ( -34.49999999999976552, -14.56887692260766443, 4.000000000000000000 ) ) ;
#67044=PLANE ( 'NONE',  #65371 ) ;
#67045=EDGE_LOOP ( 'NONE', ( #52167, #56722, #28402, #73188, #116984 ) ) ;
#67047=DIRECTION ( 'NONE',  ( 0.7071067811865487940, 0.7071067811865463515, 0.000000000000000000 ) ) ;
#67049=VECTOR ( 'NONE', #81385, 999.9999999999998863 ) ;
#67050=DIRECTION ( 'NONE',  ( -0.7071067811865486830, 0.7071067811865464625, 0.000000000000000000 ) ) ;
#67052=ADVANCED_FACE ( 'NONE', ( #61180 ), #105331, .F. ) ;
#67053=PLANE ( 'NONE',  #118129 ) ;
#67054=VECTOR ( 'NONE', #54280, 1000.000000000000000 ) ;
#67055=CARTESIAN_POINT ( 'NONE',  ( 14.29289321881336150, 8.259292476615639700, 5.000000000000000000 ) ) ;
#67057=VERTEX_POINT ( 'NONE', #83619 ) ;
#67059=ORIENTED_EDGE ( 'NONE', *, *, #55629, .T. ) ;
#67061=VECTOR ( 'NONE', #8909, 1000.000000000000000 ) ;
#67062=VECTOR ( 'NONE', #100928, 1000.000000000000000 ) ;
#67063=AXIS2_PLACEMENT_3D ( 'NONE', #107331, #61720, #138549 ) ;
#67064=DIRECTION ( 'NONE',  ( -0.7071067811865486830, -0.7071067811865464625, 0.000000000000000000 ) ) ;
#67065=CARTESIAN_POINT ( 'NONE',  ( -60.18398860626900415, 28.73617430169829490, 5.000000000000000000 ) ) ;
#67068=LINE ( 'NONE', #11945, #135747 ) ;
#67069=ORIENTED_EDGE ( 'NONE', *, *, #76467, .F. ) ;
#67070=AXIS2_PLACEMENT_3D ( 'NONE', #130601, #22489, #110928 ) ;
#67071=ORIENTED_EDGE ( 'NONE', *, *, #111850, .T. ) ;
#67072=CARTESIAN_POINT ( 'NONE',  ( -8.999999999999932498, 5.587461875839184522, 4.000000000000000000 ) ) ;
#67073=CARTESIAN_POINT ( 'NONE',  ( -12.48921356237309155, -27.52281430457064104, 5.000000000000000000 ) ) ;
#67074=VECTOR ( 'NONE', #8201, 1000.000000000000227 ) ;
#67076=DIRECTION ( 'NONE',  ( -0.7071067811865487940, 0.7071067811865463515, -0.000000000000000000 ) ) ;
#67078=PLANE ( 'NONE',  #11514 ) ;
#67079=EDGE_CURVE ( 'NONE', #22343, #90151, #12530, .T. ) ;
#67080=CARTESIAN_POINT ( 'NONE',  ( -32.67183060077623935, -6.740707523384205757, 4.000000000000000000 ) ) ;
#67083=LINE ( 'NONE', #361, #7539 ) ;
#67084=ADVANCED_FACE ( 'NONE', ( #67680 ), #112570, .F. ) ;
#67085=CARTESIAN_POINT ( 'NONE',  ( -34.49999999999976552, -1.535744391599501490, 4.994342998332164996 ) ) ;
#67086=CARTESIAN_POINT ( 'NONE',  ( -33.48921356237309510, -27.52281430457078670, 5.000000000000000000 ) ) ;
#67088=ORIENTED_EDGE ( 'NONE', *, *, #89947, .F. ) ;
#67090=ADVANCED_FACE ( 'NONE', ( #125611 ), #26286, .F. ) ;
#67091=CARTESIAN_POINT ( 'NONE',  ( 20.51078643762690490, -27.52281430457041012, 5.000000000000000000 ) ) ;
#67092=ORIENTED_EDGE ( 'NONE', *, *, #43191, .T. ) ;
#67093=FACE_OUTER_BOUND ( 'NONE', #102411, .T. ) ;
#67096=LINE ( 'NONE', #105246, #116106 ) ;
#67097=DIRECTION ( 'NONE',  ( -0.7071067811865486830, -0.7071067811865464625, 0.000000000000000000 ) ) ;
#67098=EDGE_CURVE ( 'NONE', #125881, #80563, #81405, .T. ) ;
#67099=CARTESIAN_POINT ( 'NONE',  ( 10.49999999999992539, -12.66682484999665448, -0.6294897503863688959 ) ) ;
#67100=EDGE_CURVE ( 'NONE', #71830, #12348, #23403, .T. ) ;
#67101=DIRECTION ( 'NONE',  ( -0.3543493200069163240, -0.000000000000000000, -0.9351131265310288487 ) ) ;
#67102=DIRECTION ( 'NONE',  ( -0.7071067811865487940, 0.7071067811865463515, 0.000000000000000000 ) ) ;
#67103=EDGE_LOOP ( 'NONE', ( #81386, #100946, #26116, #49703 ) ) ;
#67104=LINE ( 'NONE', #111292, #143310 ) ;
#67105=LINE ( 'NONE', #111293, #70788 ) ;
#67106=CARTESIAN_POINT ( 'NONE',  ( -24.14562793195488766, 0.06350461447050873010, 4.871950940718891232 ) ) ;
#67107=DIRECTION ( 'NONE',  ( -0.000000000000000000, -0.000000000000000000, 1.000000000000000000 ) ) ;
#67108=ORIENTED_EDGE ( 'NONE', *, *, #123740, .F. ) ;
#67109=EDGE_CURVE ( 'NONE', #104640, #114790, #56808, .T. ) ;
#67112=VERTEX_POINT ( 'NONE', #56088 ) ;
#67113=LINE ( 'NONE', #133794, #15139 ) ;
#67114=DIRECTION ( 'NONE',  ( -0.6830127018922181881, 0.6830127018922202975, -0.2588190451025214056 ) ) ;
#67115=CARTESIAN_POINT ( 'NONE',  ( -19.05000000000000071, 3.174999999999997158, 4.000000000000000000 ) ) ;
#67116=CARTESIAN_POINT ( 'NONE',  ( 30.79289321881324071, 18.75929247661552779, 5.000000000000000000 ) ) ;
#67117=ORIENTED_EDGE ( 'NONE', *, *, #141225, .T. ) ;
#67119=EDGE_CURVE ( 'NONE', #114036, #72734, #58245, .T. ) ;
#67120=LINE ( 'NONE', #75857, #86216 ) ;
#67123=LINE ( 'NONE', #33106, #9574 ) ;
#67124=LINE ( 'NONE', #124353, #80405 ) ;
#67125=ADVANCED_FACE ( 'NONE', ( #24139 ), #57499, .T. ) ;
#67126=CARTESIAN_POINT ( 'NONE',  ( 6.489213562373093325, -27.52281430457059841, 5.000000000000000000 ) ) ;
#67127=VECTOR ( 'NONE', #11683, 999.9999999999998863 ) ;
#67128=AXIS2_PLACEMENT_3D ( 'NONE', #138897, #50452, #138171 ) ;
#67130=AXIS2_PLACEMENT_3D ( 'NONE', #54691, #44556, #11857 ) ;
#67131=FACE_BOUND ( 'NONE', #117795, .T. ) ;
#67132=CARTESIAN_POINT ( 'NONE',  ( 11.99999999999992006, 15.45873954670186556, -0.03131636524296779744 ) ) ;
#67133=EDGE_CURVE ( 'NONE', #142250, #98924, #100274, .T. ) ;
#67134=FACE_OUTER_BOUND ( 'NONE', #13833, .T. ) ;
#67136=LINE ( 'NONE', #120035, #131400 ) ;
#67137=CARTESIAN_POINT ( 'NONE',  ( -33.48921356237309510, -27.52281430457078670, 5.000000000000000000 ) ) ;
#67140=VERTEX_POINT ( 'NONE', #69822 ) ;
#67141=EDGE_LOOP ( 'NONE', ( #140089, #51105, #37873, #80378 ) ) ;
#67144=CARTESIAN_POINT ( 'NONE',  ( 15.18398860626900237, 28.73617430169797871, 5.000000000000000000 ) ) ;
#67145=EDGE_LOOP ( 'NONE', ( #24985, #108663, #40466, #112894, #58280 ) ) ;
#67146=VECTOR ( 'NONE', #62447, 1000.000000000000000 ) ;
#67147=LINE ( 'NONE', #111338, #58638 ) ;
#67150=DIRECTION ( 'NONE',  ( 0.7071067811865487940, -0.7071067811865463515, 0.000000000000000000 ) ) ;
#67151=ORIENTED_EDGE ( 'NONE', *, *, #51055, .F. ) ;
#67153=LINE ( 'NONE', #1145, #40324 ) ;
#67154=LINE ( 'NONE', #36644, #24666 ) ;
#67155=CARTESIAN_POINT ( 'NONE',  ( -15.52400138585438505, 22.03583458319438648, 4.979811245910084061 ) ) ;
#67157=DIRECTION ( 'NONE',  ( -0.000000000000000000, 0.3543493200069152138, -0.9351131265310292928 ) ) ;
#67158=ORIENTED_EDGE ( 'NONE', *, *, #74815, .F. ) ;
#67160=DIRECTION ( 'NONE',  ( -0.7071067811865487940, 0.7071067811865463515, -0.000000000000000000 ) ) ;
#67161=LINE ( 'NONE', #133842, #4850 ) ;
#67162=EDGE_LOOP ( 'NONE', ( #76479, #87354, #109707, #72753 ) ) ;
#67163=ORIENTED_EDGE ( 'NONE', *, *, #28641, .T. ) ;
#67164=AXIS2_PLACEMENT_3D ( 'NONE', #27420, #127465, #51353 ) ;
#67165=ORIENTED_EDGE ( 'NONE', *, *, #29910, .F. ) ;
#67167=VECTOR ( 'NONE', #56062, 1000.000000000000000 ) ;
#67168=EDGE_LOOP ( 'NONE', ( #94935, #85996, #97299, #102485 ) ) ;
#67169=CARTESIAN_POINT ( 'NONE',  ( -4.828169399223490643, 12.75929247661559351, 4.000000000000000000 ) ) ;
#67173=CARTESIAN_POINT ( 'NONE',  ( 54.29974487139159578, -27.71228299555243879, 4.000000000000000000 ) ) ;
#67176=ORIENTED_EDGE ( 'NONE', *, *, #130768, .F. ) ;
#67177=CARTESIAN_POINT ( 'NONE',  ( -29.99999999999978328, -0.03360074219773898085, 5.000000000000000000 ) ) ;
#67178=ADVANCED_FACE ( 'NONE', ( #36443 ), #14688, .F. ) ;
#67179=VECTOR ( 'NONE', #7485, 1000.000000000000227 ) ;
#67180=PLANE ( 'NONE',  #70190 ) ;
#67181=ORIENTED_EDGE ( 'NONE', *, *, #128472, .T. ) ;
#67182=CARTESIAN_POINT ( 'NONE',  ( -38.99451991528749062, 28.92564299267965211, 4.000000000000000000 ) ) ;
#67183=FACE_OUTER_BOUND ( 'NONE', #46793, .T. ) ;
#67184=EDGE_LOOP ( 'NONE', ( #29686, #125107, #80438, #88559 ) ) ;
#67185=DIRECTION ( 'NONE',  ( -0.000000000000000000, 0.3543493200069153248, 0.9351131265310292928 ) ) ;
#67186=ORIENTED_EDGE ( 'NONE', *, *, #84744, .F. ) ;
#67187=ORIENTED_EDGE ( 'NONE', *, *, #3583, .F. ) ;
#67190=VECTOR ( 'NONE', #112466, 1000.000000000000114 ) ;
#67191=CARTESIAN_POINT ( 'NONE',  ( 39.48921356237310221, -27.52281430457082934, 5.000000000000000000 ) ) ;
#67192=ADVANCED_FACE ( 'NONE', ( #35038 ), #136453, .F. ) ;
#67193=CARTESIAN_POINT ( 'NONE',  ( 65.99451991528749772, 28.92564299267984396, 4.000000000000000000 ) ) ;
#67194=EDGE_CURVE ( 'NONE', #124937, #18835, #48755, .T. ) ;
#67195=CARTESIAN_POINT ( 'NONE',  ( 51.48921356237309510, -27.52281430457091460, 5.000000000000000000 ) ) ;
#67198=CARTESIAN_POINT ( 'NONE',  ( -6.938893903907228378E-15, -5.527737879153195699, -7.983877177622371590 ) ) ;
#67201=FACE_OUTER_BOUND ( 'NONE', #9742, .T. ) ;
#67202=ADVANCED_FACE ( 'NONE', ( #74068 ), #104542, .T. ) ;
#67203=CARTESIAN_POINT ( 'NONE',  ( -13.17183060077638324, -11.24070752338417556, 4.000000000000000000 ) ) ;
#67204=ORIENTED_EDGE ( 'NONE', *, *, #4612, .T. ) ;
#67206=ORIENTED_EDGE ( 'NONE', *, *, #28856, .F. ) ;
#67209=VECTOR ( 'NONE', #77411, 1000.000000000000227 ) ;
#67210=DIRECTION ( 'NONE',  ( 0.7071067811865487940, 0.7071067811865463515, 0.000000000000000000 ) ) ;
#67212=ADVANCED_FACE ( 'NONE', ( #95087 ), #106665, .F. ) ;
#67213=VECTOR ( 'NONE', #60952, 999.9999999999998863 ) ;
#67214=AXIS2_PLACEMENT_3D ( 'NONE', #75927, #9939, #65807 ) ;
#67215=DIRECTION ( 'NONE',  ( -0.6830127018922180770, -0.6830127018922204085, -0.2588190451025213501 ) ) ;
#67217=CARTESIAN_POINT ( 'NONE',  ( 48.29974487139158867, -27.71228299555239971, 4.000000000000000000 ) ) ;
#67218=DIRECTION ( 'NONE',  ( 0.6830127018922181881, 0.6830127018922202975, -0.2588190451025214056 ) ) ;
#67219=VERTEX_POINT ( 'NONE', #126999 ) ;
#67220=DIRECTION ( 'NONE',  ( -0.000000000000000000, -0.3543493200069152693, 0.9351131265310292928 ) ) ;
#67221=EDGE_LOOP ( 'NONE', ( #43893, #112269, #62212, #90406 ) ) ;
#67222=VECTOR ( 'NONE', #42776, 1000.000000000000000 ) ;
#67223=ADVANCED_FACE ( 'NONE', ( #26984 ), #71958, .F. ) ;
#67224=VECTOR ( 'NONE', #55827, 1000.000000000000227 ) ;
#67227=EDGE_LOOP ( 'NONE', ( #81501, #136451, #23279, #77356 ) ) ;
#67228=VECTOR ( 'NONE', #142249, 1000.000000000000227 ) ;
#67230=CARTESIAN_POINT ( 'NONE',  ( 45.18398860626900415, 28.73617430169818832, 5.000000000000000000 ) ) ;
#67231=ORIENTED_EDGE ( 'NONE', *, *, #72353, .T. ) ;
#67232=FACE_OUTER_BOUND ( 'NONE', #89224, .T. ) ;
#67233=ORIENTED_EDGE ( 'NONE', *, *, #93584, .T. ) ;
#67235=ORIENTED_EDGE ( 'NONE', *, *, #128326, .F. ) ;
#67236=CARTESIAN_POINT ( 'NONE',  ( -20.99451991528748707, 28.92564299267952777, 4.000000000000000000 ) ) ;
#67239=CARTESIAN_POINT ( 'NONE',  ( -36.48921356237310221, -27.52281430457080802, 5.000000000000000000 ) ) ;
#67242=DIRECTION ( 'NONE',  ( 0.7071067811865487940, -0.7071067811865463515, 0.000000000000000000 ) ) ;
#67243=CARTESIAN_POINT ( 'NONE',  ( -7.499999999999947597, 22.01701374228154506, 2.453858888625646273 ) ) ;
#67244=LINE ( 'NONE', #98438, #58798 ) ;
#67245=EDGE_CURVE ( 'NONE', #50205, #49451, #51616, .T. ) ;
#67246=CARTESIAN_POINT ( 'NONE',  ( 42.18398860626899705, 28.73617430169816700, 5.000000000000000000 ) ) ;
#67248=CARTESIAN_POINT ( 'NONE',  ( 15.81246187583935914, -22.22500000000000142, 4.000000000000000000 ) ) ;
#67249=VECTOR ( 'NONE', #23932, 1000.000000000000227 ) ;
#67250=CARTESIAN_POINT ( 'NONE',  ( -25.49999999999981526, 3.073033219394602611, -6.593910359671030008 ) ) ;
#67252=ORIENTED_EDGE ( 'NONE', *, *, #61176, .F. ) ;
#67253=ADVANCED_FACE ( 'NONE', ( #140055 ), #137195, .T. ) ;
#67254=ORIENTED_EDGE ( 'NONE', *, *, #112036, .F. ) ;
#67256=VECTOR ( 'NONE', #30569, 1000.000000000000000 ) ;
#67257=CARTESIAN_POINT ( 'NONE',  ( -22.49999999999984368, -1.695981523266240076, 4.571483868317929300 ) ) ;
#67258=ORIENTED_EDGE ( 'NONE', *, *, #103841, .T. ) ;
#67259=AXIS2_PLACEMENT_3D ( 'NONE', #25406, #23260, #67536 ) ;
#67261=VECTOR ( 'NONE', #112374, 1000.000000000000227 ) ;
#67262=DIRECTION ( 'NONE',  ( -0.000000000000000000, -0.3543493200069152693, 0.9351131265310292928 ) ) ;
#67263=CARTESIAN_POINT ( 'NONE',  ( 0.000000000000000000, -21.72500000000000142, 4.500000000000000888 ) ) ;
#67264=CARTESIAN_POINT ( 'NONE',  ( 33.48921356237309510, -27.52281430457078670, 5.000000000000000000 ) ) ;
#67265=CARTESIAN_POINT ( 'NONE',  ( -1.475890350552386376, 22.22500000000000142, 17.67511803955545702 ) ) ;
#67266=ORIENTED_EDGE ( 'NONE', *, *, #76020, .F. ) ;
#67267=VECTOR ( 'NONE', #101808, 1000.000000000000000 ) ;
#67268=EDGE_CURVE ( 'NONE', #108717, #8845, #115379, .T. ) ;
#67270=DIRECTION ( 'NONE',  ( 0.3543493200069162685, -0.000000000000000000, -0.9351131265310288487 ) ) ;
#67271=CARTESIAN_POINT ( 'NONE',  ( 6.183988606268994381, 28.73617430169791476, 5.000000000000000000 ) ) ;
#67272=EDGE_CURVE ( 'NONE', #122674, #15871, #39312, .T. ) ;
#67273=DIRECTION ( 'NONE',  ( -0.000000000000000000, 0.000000000000000000, 1.000000000000000000 ) ) ;
#67276=CARTESIAN_POINT ( 'NONE',  ( 33.48921356237309510, -27.52281430457078670, 5.000000000000000000 ) ) ;
#67278=CARTESIAN_POINT ( 'NONE',  ( -6.183988606268994381, 28.73617430169791476, 5.000000000000000000 ) ) ;
#67280=PLANE ( 'NONE',  #116447 ) ;
#67281=CARTESIAN_POINT ( 'NONE',  ( 8.356812572482565926, -20.24070752338407431, 21.22881796311214941 ) ) ;
#67282=LINE ( 'NONE', #66565, #35418 ) ;
#67283=ORIENTED_EDGE ( 'NONE', *, *, #46607, .T. ) ;
#67284=ORIENTED_EDGE ( 'NONE', *, *, #5607, .F. ) ;
#67285=ORIENTED_EDGE ( 'NONE', *, *, #67312, .F. ) ;
#67287=ADVANCED_FACE ( 'NONE', ( #116850 ), #139357, .F. ) ;
#67288=VECTOR ( 'NONE', #119265, 1000.000000000000000 ) ;
#67289=ORIENTED_EDGE ( 'NONE', *, *, #49454, .T. ) ;
#67290=ADVANCED_FACE ( 'NONE', ( #29129 ), #17525, .T. ) ;
#67291=PLANE ( 'NONE',  #129646 ) ;
#67292=CARTESIAN_POINT ( 'NONE',  ( -34.92500000000001137, 10.80009451602710513, 4.759050581649340472 ) ) ;
#67293=VECTOR ( 'NONE', #94862, 1000.000000000000000 ) ;
#67294=CARTESIAN_POINT ( 'NONE',  ( 39.66846741159832135, -18.74070752338409562, 20.73178291233850246 ) ) ;
#67295=DIRECTION ( 'NONE',  ( -0.000000000000000000, 0.3543493200069153248, 0.9351131265310292928 ) ) ;
#67296=VERTEX_POINT ( 'NONE', #61783 ) ;
#67297=EDGE_CURVE ( 'NONE', #83415, #121732, #84260, .T. ) ;
#67298=LINE ( 'NONE', #111493, #72292 ) ;
#67299=LINE ( 'NONE', #68052, #88234 ) ;
#67300=LINE ( 'NONE', #1286, #46578 ) ;
#67302=ORIENTED_EDGE ( 'NONE', *, *, #105038, .T. ) ;
#67303=LINE ( 'NONE', #56467, #134632 ) ;
#67305=AXIS2_PLACEMENT_3D ( 'NONE', #120269, #21715, #65249 ) ;
#67306=ORIENTED_EDGE ( 'NONE', *, *, #113987, .F. ) ;
#67307=ORIENTED_EDGE ( 'NONE', *, *, #47335, .F. ) ;
#67308=CARTESIAN_POINT ( 'NONE',  ( 72.18398860626899705, 28.73617430169837661, 5.000000000000000000 ) ) ;
#67312=EDGE_CURVE ( 'NONE', #20345, #14571, #137909, .T. ) ;
#67313=AXIS2_PLACEMENT_3D ( 'NONE', #127131, #103239, #50309 ) ;
#67314=VECTOR ( 'NONE', #121735, 1000.000000000000000 ) ;
#67315=CARTESIAN_POINT ( 'NONE',  ( 9.005480084712511157, 28.92564299267931816, 4.000000000000000000 ) ) ;
#67316=DIRECTION ( 'NONE',  ( 0.6830127018922180770, -0.6830127018922204085, -0.2588190451025213501 ) ) ;
#67317=EDGE_CURVE ( 'NONE', #4021, #85291, #73370, .T. ) ;
#67318=CARTESIAN_POINT ( 'NONE',  ( 33.29974487139158867, -27.71228299555229313, 4.000000000000000000 ) ) ;
#67320=EDGE_CURVE ( 'NONE', #126030, #136740, #117537, .T. ) ;
#67323=DIRECTION ( 'NONE',  ( 0.000000000000000000, 0.000000000000000000, -1.000000000000000000 ) ) ;
#67324=EDGE_LOOP ( 'NONE', ( #34129, #86241, #36327 ) ) ;
#67325=ORIENTED_EDGE ( 'NONE', *, *, #24287, .T. ) ;
#67327=EDGE_CURVE ( 'NONE', #47375, #57071, #75498, .T. ) ;
#67328=VECTOR ( 'NONE', #118093, 999.9999999999998863 ) ;
#67329=VECTOR ( 'NONE', #61960, 1000.000000000000227 ) ;
#67330=DIRECTION ( 'NONE',  ( -0.6830127018922180770, -0.6830127018922204085, -0.2588190451025214056 ) ) ;
#67331=ORIENTED_EDGE ( 'NONE', *, *, #31858, .F. ) ;
#67332=CARTESIAN_POINT ( 'NONE',  ( -68.99451991528748351, 28.92564299267986172, 4.000000000000000000 ) ) ;
#67333=DIRECTION ( 'NONE',  ( 0.6830127018922180770, -0.6830127018922204085, -0.2588190451025213501 ) ) ;
#67334=CARTESIAN_POINT ( 'NONE',  ( 34.47516574401890921, -19.50948238788418010, 4.998110765256834398 ) ) ;
#67336=AXIS2_PLACEMENT_3D ( 'NONE', #5110, #70465, #16738 ) ;
#67339=CIRCLE ( 'NONE', #76559, 3.378199999999997871 ) ;
#67341=ORIENTED_EDGE ( 'NONE', *, *, #69191, .F. ) ;
#67342=VECTOR ( 'NONE', #279, 1000.000000000000000 ) ;
#67343=ORIENTED_EDGE ( 'NONE', *, *, #26821, .T. ) ;
#67344=PLANE ( 'NONE',  #73561 ) ;
#67345=ORIENTED_EDGE ( 'NONE', *, *, #103777, .F. ) ;
#67346=CARTESIAN_POINT ( 'NONE',  ( -16.49999999999987566, 22.08746187583901843, 4.000000000000000000 ) ) ;
#67347=VERTEX_POINT ( 'NONE', #19 ) ;
#67348=CARTESIAN_POINT ( 'NONE',  ( -5.510786437626906675, -27.52281430457051314, 5.000000000000000000 ) ) ;
#67350=ORIENTED_EDGE ( 'NONE', *, *, #26524, .F. ) ;
#67352=ORIENTED_EDGE ( 'NONE', *, *, #21015, .T. ) ;
#67353=DIRECTION ( 'NONE',  ( 0.7071067811865487940, 0.7071067811865463515, 0.000000000000000000 ) ) ;
#67354=LINE ( 'NONE', #111546, #29798 ) ;
#67355=DIRECTION ( 'NONE',  ( 0.7071067811865487940, 0.7071067811865463515, -0.000000000000000000 ) ) ;
#67357=CARTESIAN_POINT ( 'NONE',  ( 15.79289321881335795, -8.240707523384193323, 5.000000000000000000 ) ) ;
#67358=VECTOR ( 'NONE', #128299, 999.9999999999998863 ) ;
#67359=ADVANCED_FACE ( 'NONE', ( #88524 ), #8746, .F. ) ;
#67360=LINE ( 'NONE', #89110, #89927 ) ;
#67361=VECTOR ( 'NONE', #67220, 1000.000000000000000 ) ;
#67362=CYLINDRICAL_SURFACE ( 'NONE', #123466, 0.5000000000000004441 ) ;
#67363=AXIS2_PLACEMENT_3D ( 'NONE', #48780, #13967, #3108 ) ;
#67364=CARTESIAN_POINT ( 'NONE',  ( 17.99999999999986855, -18.41253812416056945, 4.000000000000000000 ) ) ;
#67365=ORIENTED_EDGE ( 'NONE', *, *, #12432, .T. ) ;
#67366=AXIS2_PLACEMENT_3D ( 'NONE', #50343, #15520, #38048 ) ;
#67367=LINE ( 'NONE', #57218, #98980 ) ;
#67368=FACE_OUTER_BOUND ( 'NONE', #44449, .T. ) ;
#67369=DIRECTION ( 'NONE',  ( -0.000000000000000000, 0.3543493200069153248, 0.9351131265310292928 ) ) ;
#67372=ORIENTED_EDGE ( 'NONE', *, *, #108060, .T. ) ;
#67373=ORIENTED_EDGE ( 'NONE', *, *, #34181, .T. ) ;
#67374=LINE ( 'NONE', #12245, #56453 ) ;
#67376=AXIS2_PLACEMENT_3D ( 'NONE', #44257, #55849, #122488 ) ;
#67377=EDGE_CURVE ( 'NONE', #35802, #101026, #96486, .T. ) ;
#67379=CARTESIAN_POINT ( 'NONE',  ( -17.30701457986679870, -22.22500000000000142, -1.676113270567823221 ) ) ;
#67380=CARTESIAN_POINT ( 'NONE',  ( 34.49999999999975842, -17.94567065516886117, 4.994342998332151673 ) ) ;
#67381=EDGE_CURVE ( 'NONE', #45124, #37390, #31288, .T. ) ;
#67382=AXIS2_PLACEMENT_3D ( 'NONE', #48867, #82924, #27808 ) ;
#67383=LINE ( 'NONE', #110126, #72733 ) ;
#67384=LINE ( 'NONE', #34743, #76556 ) ;
#67386=DIRECTION ( 'NONE',  ( -0.3543493200069162685, -0.000000000000000000, -0.9351131265310288487 ) ) ;
#67387=ORIENTED_EDGE ( 'NONE', *, *, #33529, .T. ) ;
#67388=DIRECTION ( 'NONE',  ( -0.7071067811865487940, 0.7071067811865463515, -0.000000000000000000 ) ) ;
#67389=EDGE_CURVE ( 'NONE', #139347, #36309, #21098, .T. ) ;
#67390=ADVANCED_FACE ( 'NONE', ( #33452 ), #108079, .T. ) ;
#67391=VECTOR ( 'NONE', #37545, 1000.000000000000000 ) ;
#67393=ORIENTED_EDGE ( 'NONE', *, *, #11709, .T. ) ;
#67395=DIRECTION ( 'NONE',  ( -0.7071067811865486830, 0.7071067811865464625, 0.000000000000000000 ) ) ;
#67396=ADVANCED_FACE ( 'NONE', ( #30573 ), #64613, .T. ) ;
#67397=DIRECTION ( 'NONE',  ( 0.6830127018922180770, -0.6830127018922204085, -0.2588190451025213501 ) ) ;
#67399=ORIENTED_EDGE ( 'NONE', *, *, #138091, .F. ) ;
#67400=VECTOR ( 'NONE', #22825, 1000.000000000000227 ) ;
#67401=ORIENTED_EDGE ( 'NONE', *, *, #68057, .F. ) ;
#67402=CARTESIAN_POINT ( 'NONE',  ( 8.816011393731004731, 28.73617430169781173, 5.000000000000000000 ) ) ;
#67403=DIRECTION ( 'NONE',  ( 0.7071067811865486830, -0.7071067811865464625, -0.000000000000000000 ) ) ;
#67404=LINE ( 'NONE', #99257, #39583 ) ;
#67405=CARTESIAN_POINT ( 'NONE',  ( -3.758600742197928835, 21.72499999999999432, 5.000000000000000000 ) ) ;
#67406=VECTOR ( 'NONE', #39961, 1000.000000000000227 ) ;
#67407=FACE_OUTER_BOUND ( 'NONE', #37790, .T. ) ;
#67408=ORIENTED_EDGE ( 'NONE', *, *, #26505, .T. ) ;
#67410=ADVANCED_FACE ( 'NONE', ( #10217 ), #98657, .F. ) ;
#67412=LINE ( 'NONE', #98577, #51457 ) ;
#67413=ORIENTED_EDGE ( 'NONE', *, *, #120898, .T. ) ;
#67415=VECTOR ( 'NONE', #103359, 1000.000000000000000 ) ;
#67416=ADVANCED_FACE ( 'NONE', ( #43571 ), #42170, .F. ) ;
#67417=CARTESIAN_POINT ( 'NONE',  ( -54.29974487139159578, -27.71228299555243879, 4.000000000000000000 ) ) ;
#67418=ORIENTED_EDGE ( 'NONE', *, *, #89427, .T. ) ;
#67419=DIRECTION ( 'NONE',  ( -0.7071067811865486830, -0.7071067811865464625, 0.000000000000000000 ) ) ;
#67420=ORIENTED_EDGE ( 'NONE', *, *, #20684, .F. ) ;
#67421=ORIENTED_EDGE ( 'NONE', *, *, #91009, .F. ) ;
#67422=CARTESIAN_POINT ( 'NONE',  ( -32.99999999999976552, -16.02097659208073566, -11.96015758381200733 ) ) ;
#67423=PLANE ( 'NONE',  #4354 ) ;
#67424=EDGE_CURVE ( 'NONE', #30921, #109630, #142886, .T. ) ;
#67425=AXIS2_PLACEMENT_3D ( 'NONE', #42135, #129831, #42847 ) ;
#67427=CARTESIAN_POINT ( 'NONE',  ( -27.18398860626900060, 28.73617430169806042, 5.000000000000000000 ) ) ;
#67428=DIRECTION ( 'NONE',  ( 0.7071067811865486830, -0.7071067811865464625, -0.000000000000000000 ) ) ;
#67429=LINE ( 'NONE', #14451, #76405 ) ;
#67430=CARTESIAN_POINT ( 'NONE',  ( -69.48921356237309510, -27.52281430457103895, 5.000000000000000000 ) ) ;
#67432=CARTESIAN_POINT ( 'NONE',  ( 36.48921356237310221, -27.52281430457080802, 5.000000000000000000 ) ) ;
#67433=CARTESIAN_POINT ( 'NONE',  ( 18.60486233187509697, 21.75929247661549226, 21.32995629748182154 ) ) ;
#67434=LINE ( 'NONE', #56588, #93398 ) ;
#67435=EDGE_CURVE ( 'NONE', #32728, #122903, #118989, .T. ) ;
#67436=LINE ( 'NONE', #111633, #103867 ) ;
#67438=DIRECTION ( 'NONE',  ( -0.3543493200069163240, 0.000000000000000000, 0.9351131265310288487 ) ) ;
#67439=FACE_OUTER_BOUND ( 'NONE', #131415, .T. ) ;
#67440=VECTOR ( 'NONE', #99251, 1000.000000000000000 ) ;
#67441=CARTESIAN_POINT ( 'NONE',  ( -39.18398860626899705, 28.73617430169814568, 5.000000000000000000 ) ) ;
#67442=DIRECTION ( 'NONE',  ( 0.6830127018922180770, -0.6830127018922204085, -0.2588190451025213501 ) ) ;
#67443=ORIENTED_EDGE ( 'NONE', *, *, #7716, .T. ) ;
#67444=ORIENTED_EDGE ( 'NONE', *, *, #71199, .F. ) ;
#67445=AXIS2_PLACEMENT_3D ( 'NONE', #107776, #41113, #32395 ) ;
#67446=EDGE_CURVE ( 'NONE', #23445, #58187, #74811, .T. ) ;
#67448=VECTOR ( 'NONE', #5583, 999.9999999999998863 ) ;
#67449=VERTEX_POINT ( 'NONE', #41424 ) ;
#67451=EDGE_CURVE ( 'NONE', #22127, #49472, #32721, .T. ) ;
#67453=CARTESIAN_POINT ( 'NONE',  ( 34.45011844616451668, -5.997695858405997171, 5.000000000000000888 ) ) ;
#67454=LINE ( 'NONE', #79055, #78853 ) ;
#67455=AXIS2_PLACEMENT_3D ( 'NONE', #89835, #111604, #1380 ) ;
#67456=CIRCLE ( 'NONE', #85944, 5.968999999999998529 ) ;
#67457=AXIS2_PLACEMENT_3D ( 'NONE', #50112, #73296, #94306 ) ;
#67458=VECTOR ( 'NONE', #44115, 1000.000000000000000 ) ;
#67459=CARTESIAN_POINT ( 'NONE',  ( -34.17183060077623935, 3.759292476615681888, 4.000000000000000000 ) ) ;
#67460=ORIENTED_EDGE ( 'NONE', *, *, #59959, .F. ) ;
#67461=LINE ( 'NONE', #13728, #30089 ) ;
#67463=VECTOR ( 'NONE', #3153, 1000.000000000000000 ) ;
#67464=FACE_OUTER_BOUND ( 'NONE', #84312, .T. ) ;
#67466=DIRECTION ( 'NONE',  ( 0.7071067811865487940, 0.7071067811865463515, 0.000000000000000000 ) ) ;
#67467=VERTEX_POINT ( 'NONE', #97200 ) ;
#67469=FACE_OUTER_BOUND ( 'NONE', #78983, .T. ) ;
#67470=LINE ( 'NONE', #134134, #5616 ) ;
#67471=CARTESIAN_POINT ( 'NONE',  ( 31.49999999999979039, 19.46639925780206326, 5.000000000000000000 ) ) ;
#67472=DIRECTION ( 'NONE',  ( -0.000000000000000000, -0.3543493200069152693, 0.9351131265310292928 ) ) ;
#67473=CARTESIAN_POINT ( 'NONE',  ( -1.499999999999994449, 22.22500000000000142, 4.362957392718788796 ) ) ;
#67474=CARTESIAN_POINT ( 'NONE',  ( -20.70025512860841133, -27.71228299555191654, 4.000000000000000000 ) ) ;
#67475=LINE ( 'NONE', #90639, #49888 ) ;
#67477=ORIENTED_EDGE ( 'NONE', *, *, #133816, .T. ) ;
#67478=VERTEX_POINT ( 'NONE', #141466 ) ;
#67480=VERTEX_POINT ( 'NONE', #97961 ) ;
#67481=ADVANCED_FACE ( 'NONE', ( #21822 ), #110227, .F. ) ;
#67482=DIRECTION ( 'NONE',  ( 0.7071067811865487940, 0.7071067811865463515, 0.000000000000000000 ) ) ;
#67483=FACE_OUTER_BOUND ( 'NONE', #114764, .T. ) ;
#67484=ADVANCED_FACE ( 'NONE', ( #11620 ), #34138, .T. ) ;
#67488=VECTOR ( 'NONE', #110590, 1000.000000000000000 ) ;
#67490=ORIENTED_EDGE ( 'NONE', *, *, #121701, .T. ) ;
#67491=VECTOR ( 'NONE', #29517, 999.9999999999998863 ) ;
#67492=ORIENTED_EDGE ( 'NONE', *, *, #106476, .T. ) ;
#67493=LINE ( 'NONE', #111684, #94762 ) ;
#67494=VECTOR ( 'NONE', #133930, 1000.000000000000000 ) ;
#67495=DIRECTION ( 'NONE',  ( -0.6830127018922180770, -0.6830127018922204085, -0.2588190451025213501 ) ) ;
#67496=ORIENTED_EDGE ( 'NONE', *, *, #108806, .F. ) ;
#67497=ORIENTED_EDGE ( 'NONE', *, *, #137661, .F. ) ;
#67499=ORIENTED_EDGE ( 'NONE', *, *, #135915, .T. ) ;
#67500=VECTOR ( 'NONE', #119283, 1000.000000000000000 ) ;
#67501=FACE_OUTER_BOUND ( 'NONE', #121649, .T. ) ;
#67502=FACE_OUTER_BOUND ( 'NONE', #9710, .T. ) ;
#67504=VECTOR ( 'NONE', #100485, 999.9999999999998863 ) ;
#67506=ORIENTED_EDGE ( 'NONE', *, *, #99262, .T. ) ;
#67509=ORIENTED_EDGE ( 'NONE', *, *, #56708, .T. ) ;
#67510=VECTOR ( 'NONE', #110921, 1000.000000000000000 ) ;
#67511=ORIENTED_EDGE ( 'NONE', *, *, #26766, .T. ) ;
#67513=CARTESIAN_POINT ( 'NONE',  ( 34.42499999999998295, -22.22500000000000142, 5.000000000000000000 ) ) ;
#67515=ORIENTED_EDGE ( 'NONE', *, *, #129540, .T. ) ;
#67516=CARTESIAN_POINT ( 'NONE',  ( 5.501836514860404037, -17.24070752338409918, 8.407044977365213612 ) ) ;
#67517=DIRECTION ( 'NONE',  ( 1.000000000000000000, 0.000000000000000000, 0.000000000000000000 ) ) ;
#67518=AXIS2_PLACEMENT_3D ( 'NONE', #130880, #75773, #98233 ) ;
#67519=CARTESIAN_POINT ( 'NONE',  ( -31.44665057663198482, 2.259292476615694323, 14.86850063742361705 ) ) ;
#67520=CARTESIAN_POINT ( 'NONE',  ( -5.671830600776424092, -18.74070752338409207, 4.000000000000000000 ) ) ;
#67521=FACE_BOUND ( 'NONE', #143486, .T. ) ;
#67522=ORIENTED_EDGE ( 'NONE', *, *, #60411, .T. ) ;
#67523=DIRECTION ( 'NONE',  ( 1.000000000000000000, 0.000000000000000000, 0.000000000000000000 ) ) ;
#67524=LINE ( 'NONE', #14542, #29949 ) ;
#67525=CARTESIAN_POINT ( 'NONE',  ( 14.30673006690391702, -3.740707523384251942, 12.88036043432864020 ) ) ;
#67526=FACE_OUTER_BOUND ( 'NONE', #13874, .T. ) ;
#67527=ORIENTED_EDGE ( 'NONE', *, *, #120584, .T. ) ;
#67529=VERTEX_POINT ( 'NONE', #22496 ) ;
#67530=VERTEX_POINT ( 'NONE', #135594 ) ;
#67536=DIRECTION ( 'NONE',  ( -0.7071067811865486830, 0.7071067811865464625, 0.000000000000000000 ) ) ;
#67537=CARTESIAN_POINT ( 'NONE',  ( 23.91508676806224187, -12.74070752338414536, 18.74364270924359843 ) ) ;
#67538=ORIENTED_EDGE ( 'NONE', *, *, #37997, .T. ) ;
#67539=VECTOR ( 'NONE', #42459, 1000.000000000000000 ) ;
#67540=VECTOR ( 'NONE', #69890, 999.9999999999998863 ) ;
#67541=VECTOR ( 'NONE', #66993, 1000.000000000000000 ) ;
#67542=AXIS2_PLACEMENT_3D ( 'NONE', #141671, #9701, #119180 ) ;
#67544=DIRECTION ( 'NONE',  ( 0.6830127018922181881, 0.6830127018922202975, -0.2588190451025214056 ) ) ;
#67545=FACE_OUTER_BOUND ( 'NONE', #129931, .T. ) ;
#67546=CARTESIAN_POINT ( 'NONE',  ( 63.48921356237309510, -27.52281430457099631, 5.000000000000000000 ) ) ;
#67547=ORIENTED_EDGE ( 'NONE', *, *, #40358, .T. ) ;
#67548=EDGE_CURVE ( 'NONE', #28316, #89814, #12359, .T. ) ;
#67549=ORIENTED_EDGE ( 'NONE', *, *, #100458, .T. ) ;
#67550=VECTOR ( 'NONE', #81692, 999.9999999999998863 ) ;
#67551=VECTOR ( 'NONE', #39820, 1000.000000000000000 ) ;
#67552=ORIENTED_EDGE ( 'NONE', *, *, #6913, .T. ) ;
#67553=AXIS2_PLACEMENT_3D ( 'NONE', #23145, #68854, #101444 ) ;
#67554=VERTEX_POINT ( 'NONE', #79100 ) ;
#67555=LINE ( 'NONE', #89967, #31117 ) ;
#67556=LINE ( 'NONE', #121177, #104656 ) ;
#67557=EDGE_LOOP ( 'NONE', ( #57962, #106031, #126810, #98187, #103084 ) ) ;
#67558=VECTOR ( 'NONE', #68302, 1000.000000000000000 ) ;
#67559=ORIENTED_EDGE ( 'NONE', *, *, #51807, .T. ) ;
#67560=DIRECTION ( 'NONE',  ( -0.7071067811865486830, -0.7071067811865464625, -0.000000000000000000 ) ) ;
#67561=DIRECTION ( 'NONE',  ( -0.000000000000000000, -0.000000000000000000, 1.000000000000000000 ) ) ;
#67562=EDGE_CURVE ( 'NONE', #31625, #18811, #24664, .T. ) ;
#67564=LINE ( 'NONE', #112464, #117981 ) ;
#67566=PLANE ( 'NONE',  #104305 ) ;
#67567=CARTESIAN_POINT ( 'NONE',  ( 23.24240614354803114, -1.100504885936606669, 4.183743008713594058 ) ) ;
#67569=EDGE_CURVE ( 'NONE', #51167, #137268, #14509, .T. ) ;
#67573=ADVANCED_FACE ( 'NONE', ( #90670 ), #69642, .F. ) ;
#67576=CARTESIAN_POINT ( 'NONE',  ( 21.48921356237309155, -27.52281430457070499, 5.000000000000000000 ) ) ;
#67577=CARTESIAN_POINT ( 'NONE',  ( 24.48921356237309510, -27.52281430457072631, 5.000000000000000000 ) ) ;
#67578=ORIENTED_EDGE ( 'NONE', *, *, #29661, .F. ) ;
#67579=DIRECTION ( 'NONE',  ( -0.000000000000000000, 0.000000000000000000, 1.000000000000000000 ) ) ;
#67581=EDGE_CURVE ( 'NONE', #8995, #29676, #91384, .T. ) ;
#67582=DIRECTION ( 'NONE',  ( 0.6830127018922181881, 0.6830127018922202975, -0.2588190451025214056 ) ) ;
#67583=DIRECTION ( 'NONE',  ( 0.7071067811865487940, -0.7071067811865463515, 0.000000000000000000 ) ) ;
#67584=DIRECTION ( 'NONE',  ( 0.7071067811865487940, 0.7071067811865463515, 0.000000000000000000 ) ) ;
#67585=ORIENTED_EDGE ( 'NONE', *, *, #85527, .F. ) ;
#67587=FACE_OUTER_BOUND ( 'NONE', #142692, .T. ) ;
#67588=ADVANCED_FACE ( 'NONE', ( #25372 ), #2908, .T. ) ;
#67589=VECTOR ( 'NONE', #98331, 1000.000000000000000 ) ;
#67591=DIRECTION ( 'NONE',  ( -0.7071067811865487940, 0.7071067811865463515, -0.000000000000000000 ) ) ;
#67592=LINE ( 'NONE', #111782, #111565 ) ;
#67593=VERTEX_POINT ( 'NONE', #35595 ) ;
#67595=DIRECTION ( 'NONE',  ( 0.7071067811865487940, 0.7071067811865463515, 0.000000000000000000 ) ) ;
#67596=VERTEX_POINT ( 'NONE', #79822 ) ;
#67597=EDGE_CURVE ( 'NONE', #102769, #139749, #47891, .T. ) ;
#67598=DIRECTION ( 'NONE',  ( -0.3543493200069162685, -0.000000000000000000, -0.9351131265310288487 ) ) ;
#67599=CARTESIAN_POINT ( 'NONE',  ( 14.99999999999990230, -16.02097659208069658, -11.96015758381211924 ) ) ;
#67600=ORIENTED_EDGE ( 'NONE', *, *, #46495, .F. ) ;
#67601=ORIENTED_EDGE ( 'NONE', *, *, #97226, .T. ) ;
#67602=CARTESIAN_POINT ( 'NONE',  ( -13.10966639810773771, 3.759292476615678336, 4.164048746910666843 ) ) ;
#67604=ADVANCED_FACE ( 'NONE', ( #67501 ), #124701, .F. ) ;
#67605=ORIENTED_EDGE ( 'NONE', *, *, #80794, .T. ) ;
#67606=DIRECTION ( 'NONE',  ( -0.7071067811865486830, -0.7071067811865464625, -0.000000000000000000 ) ) ;
#67608=CARTESIAN_POINT ( 'NONE',  ( 18.72281430457046270, -21.72500000000000142, 5.000000000000000000 ) ) ;
#67609=ORIENTED_EDGE ( 'NONE', *, *, #7920, .F. ) ;
#67610=LINE ( 'NONE', #123416, #85987 ) ;
#67611=CARTESIAN_POINT ( 'NONE',  ( 19.49999999999986500, 16.18958161055405043, -11.56426086740806802 ) ) ;
#67612=AXIS2_PLACEMENT_3D ( 'NONE', #58043, #70357, #59464 ) ;
#67614=ADVANCED_FACE ( 'NONE', ( #47205 ), #77653, .F. ) ;
#67615=VECTOR ( 'NONE', #99461, 1000.000000000000000 ) ;
#67619=ORIENTED_EDGE ( 'NONE', *, *, #36600, .F. ) ;
#67620=ORIENTED_EDGE ( 'NONE', *, *, #100449, .F. ) ;
#67621=ORIENTED_EDGE ( 'NONE', *, *, #125138, .F. ) ;
#67622=EDGE_CURVE ( 'NONE', #29169, #73773, #55904, .T. ) ;
#67624=ORIENTED_EDGE ( 'NONE', *, *, #141851, .F. ) ;
#67625=EDGE_LOOP ( 'NONE', ( #111438, #14287, #105468, #129845 ) ) ;
#67627=ORIENTED_EDGE ( 'NONE', *, *, #40962, .F. ) ;
#67628=LINE ( 'NONE', #33568, #94187 ) ;
#67629=DIRECTION ( 'NONE',  ( 0.7071067811865487940, 0.7071067811865463515, 0.000000000000000000 ) ) ;
#67630=VERTEX_POINT ( 'NONE', #111691 ) ;
#67631=EDGE_CURVE ( 'NONE', #89838, #29880, #1461, .T. ) ;
#67632=PLANE ( 'NONE',  #80931 ) ;
#67633=PLANE ( 'NONE',  #81426 ) ;
#67634=EDGE_CURVE ( 'NONE', #104233, #105152, #137737, .T. ) ;
#67635=CARTESIAN_POINT ( 'NONE',  ( -13.49999999999990052, 15.05218569542901363, 5.000000000000000000 ) ) ;
#67636=PLANE ( 'NONE',  #60394 ) ;
#67638=ORIENTED_EDGE ( 'NONE', *, *, #141379, .F. ) ;
#67639=DIRECTION ( 'NONE',  ( -0.7071067811865487940, 0.7071067811865463515, -0.000000000000000000 ) ) ;
#67640=CARTESIAN_POINT ( 'NONE',  ( -7.001930566820925961, -22.22500000000000142, 4.500000000000000888 ) ) ;
#67641=LINE ( 'NONE', #111835, #105088 ) ;
#67643=CARTESIAN_POINT ( 'NONE',  ( 26.99451991528749417, 28.92564299267956685, 4.000000000000000000 ) ) ;
#67644=FACE_OUTER_BOUND ( 'NONE', #108612, .T. ) ;
#67648=LINE ( 'NONE', #102408, #125523 ) ;
#67649=FACE_OUTER_BOUND ( 'NONE', #82852, .T. ) ;
#67650=ORIENTED_EDGE ( 'NONE', *, *, #89283, .F. ) ;
#67654=PLANE ( 'NONE',  #134340 ) ;
#67655=DIRECTION ( 'NONE',  ( 0.6830127018922181881, 0.6830127018922202975, -0.2588190451025214056 ) ) ;
#67656=ORIENTED_EDGE ( 'NONE', *, *, #69741, .T. ) ;
#67659=VECTOR ( 'NONE', #7891, 1000.000000000000227 ) ;
#67660=DIRECTION ( 'NONE',  ( -0.7071067811865486830, -0.7071067811865464625, 0.000000000000000000 ) ) ;
#67661=FACE_OUTER_BOUND ( 'NONE', #94313, .T. ) ;
#67662=VECTOR ( 'NONE', #107097, 1000.000000000000000 ) ;
#67665=EDGE_CURVE ( 'NONE', #66690, #12661, #62318, .T. ) ;
#67666=EDGE_LOOP ( 'NONE', ( #129689, #23610, #12246, #80163 ) ) ;
#67667=DIRECTION ( 'NONE',  ( 0.3543493200069162685, -0.000000000000000000, -0.9351131265310288487 ) ) ;
#67668=ORIENTED_EDGE ( 'NONE', *, *, #61374, .T. ) ;
#67670=AXIS2_PLACEMENT_3D ( 'NONE', #107712, #105561, #29436 ) ;
#67671=VECTOR ( 'NONE', #51203, 1000.000000000000227 ) ;
#67673=CYLINDRICAL_SURFACE ( 'NONE', #58916, 0.5000000000000004441 ) ;
#67674=DIRECTION ( 'NONE',  ( -0.7071067811865487940, 0.7071067811865463515, 0.000000000000000000 ) ) ;
#67675=DIRECTION ( 'NONE',  ( -0.7071067811865486830, -0.7071067811865463515, 0.000000000000000000 ) ) ;
#67676=ORIENTED_EDGE ( 'NONE', *, *, #36841, .F. ) ;
#67677=EDGE_CURVE ( 'NONE', #111310, #57451, #130230, .T. ) ;
#67678=DIRECTION ( 'NONE',  ( -0.7071067811865486830, -0.7071067811865464625, -0.000000000000000000 ) ) ;
#67679=EDGE_LOOP ( 'NONE', ( #12921, #68632, #28342, #39074 ) ) ;
#67680=FACE_OUTER_BOUND ( 'NONE', #141638, .T. ) ;
#67682=FACE_OUTER_BOUND ( 'NONE', #125835, .T. ) ;
#67683=CARTESIAN_POINT ( 'NONE',  ( -72.18398860626899705, 28.73617430169837661, 5.000000000000000000 ) ) ;
#67684=CARTESIAN_POINT ( 'NONE',  ( -23.60898926630779826, -0.6778661889157658882, 4.000000000000000000 ) ) ;
#67685=EDGE_CURVE ( 'NONE', #108226, #101224, #60922, .T. ) ;
#67686=ORIENTED_EDGE ( 'NONE', *, *, #63323, .T. ) ;
#67687=CARTESIAN_POINT ( 'NONE',  ( -15.48921356237309510, -27.52281430457066236, 5.000000000000000000 ) ) ;
#67689=CARTESIAN_POINT ( 'NONE',  ( -29.52663903635766829, -5.240707523384225297, 16.25846745537488758 ) ) ;
#67690=CARTESIAN_POINT ( 'NONE',  ( 14.81601139373099585, 28.73617430169776910, 5.000000000000000000 ) ) ;
#67693=LINE ( 'NONE', #25565, #130305 ) ;
#67695=ORIENTED_EDGE ( 'NONE', *, *, #23351, .F. ) ;
#67697=AXIS2_PLACEMENT_3D ( 'NONE', #56495, #91243, #58649 ) ;
#67698=VECTOR ( 'NONE', #72529, 999.9999999999998863 ) ;
#67699=EDGE_CURVE ( 'NONE', #70301, #11420, #116673, .T. ) ;
#67700=FACE_OUTER_BOUND ( 'NONE', #127959, .T. ) ;
#67701=ORIENTED_EDGE ( 'NONE', *, *, #21636, .T. ) ;
#67702=AXIS2_PLACEMENT_3D ( 'NONE', #115096, #15092, #25998 ) ;
#67703=LINE ( 'NONE', #48063, #42283 ) ;
#67704=DIRECTION ( 'NONE',  ( -1.000000000000000000, 0.000000000000000000, 0.000000000000000000 ) ) ;
#67705=CARTESIAN_POINT ( 'NONE',  ( -10.99806943317894437, -22.22500000000000142, 4.500000000000000888 ) ) ;
#67706=VECTOR ( 'NONE', #97170, 1000.000000000000000 ) ;
#67707=CARTESIAN_POINT ( 'NONE',  ( -3.328169399223500413, 14.25929247661557575, 4.000000000000000000 ) ) ;
#67708=FACE_BOUND ( 'NONE', #74658, .T. ) ;
#67709=EDGE_CURVE ( 'NONE', #56788, #87398, #81953, .T. ) ;
#67710=CARTESIAN_POINT ( 'NONE',  ( -14.24715658456393541, 6.719242673238161601, 5.000000000000000000 ) ) ;
#67711=LINE ( 'NONE', #69113, #32767 ) ;
#67712=DIRECTION ( 'NONE',  ( 0.7071067811865486830, -0.7071067811865464625, -0.000000000000000000 ) ) ;
#67713=CARTESIAN_POINT ( 'NONE',  ( 0.000000000000000000, 21.72500000000000142, 4.500000000000000888 ) ) ;
#67714=EDGE_LOOP ( 'NONE', ( #92676, #138450, #17837, #122646 ) ) ;
#67715=DIRECTION ( 'NONE',  ( 0.6830127018922181881, 0.6830127018922202975, -0.2588190451025214056 ) ) ;
#67716=VERTEX_POINT ( 'NONE', #37715 ) ;
#67717=ORIENTED_EDGE ( 'NONE', *, *, #82196, .F. ) ;
#67719=ORIENTED_EDGE ( 'NONE', *, *, #28322, .T. ) ;
#67720=DIRECTION ( 'NONE',  ( 0.6830127018922180770, 0.6830127018922202975, -0.2588190451025213501 ) ) ;
#67721=DIRECTION ( 'NONE',  ( 0.3543493200069162685, -0.000000000000000000, -0.9351131265310288487 ) ) ;
#67723=ORIENTED_EDGE ( 'NONE', *, *, #74287, .T. ) ;
#67724=DIRECTION ( 'NONE',  ( -0.000000000000000000, 0.3543493200069153248, 0.9351131265310292928 ) ) ;
#67725=VECTOR ( 'NONE', #91326, 1000.000000000000000 ) ;
#67727=FACE_OUTER_BOUND ( 'NONE', #120841, .T. ) ;
#67729=DIRECTION ( 'NONE',  ( 0.7071067811865487940, 0.7071067811865463515, 0.000000000000000000 ) ) ;
#67730=CARTESIAN_POINT ( 'NONE',  ( 15.18398860626900237, 28.73617430169797871, 5.000000000000000000 ) ) ;
#67732=ORIENTED_EDGE ( 'NONE', *, *, #82503, .F. ) ;
#67733=VECTOR ( 'NONE', #5831, 1000.000000000000000 ) ;
#67739=VERTEX_POINT ( 'NONE', #83346 ) ;
#67741=EDGE_CURVE ( 'NONE', #129269, #115465, #110957, .T. ) ;
#67743=VECTOR ( 'NONE', #140699, 1000.000000000000000 ) ;
#67744=ORIENTED_EDGE ( 'NONE', *, *, #36552, .F. ) ;
#67745=DIRECTION ( 'NONE',  ( -0.000000000000000000, 0.3543493200069153248, 0.9351131265310292928 ) ) ;
#67746=DIRECTION ( 'NONE',  ( -0.000000000000000000, -0.3543493200069152693, 0.9351131265310292928 ) ) ;
#67747=EDGE_CURVE ( 'NONE', #141224, #7871, #50715, .T. ) ;
#67748=ADVANCED_FACE ( 'NONE', ( #94902 ), #28960, .F. ) ;
#67750=DIRECTION ( 'NONE',  ( -0.000000000000000000, 0.3543493200069153248, 0.9351131265310292928 ) ) ;
#67751=EDGE_CURVE ( 'NONE', #15312, #30859, #117363, .T. ) ;
#67752=EDGE_LOOP ( 'NONE', ( #132499, #64802, #116292 ) ) ;
#67753=DIRECTION ( 'NONE',  ( -0.7071067811865487940, 0.7071067811865463515, 0.000000000000000000 ) ) ;
#67755=PLANE ( 'NONE',  #99808 ) ;
#67756=DIRECTION ( 'NONE',  ( 0.7071067811865487940, 0.7071067811865463515, 0.000000000000000000 ) ) ;
#67757=VECTOR ( 'NONE', #34969, 1000.000000000000227 ) ;
#67758=AXIS2_PLACEMENT_3D ( 'NONE', #87351, #22754, #131567 ) ;
#67759=PLANE ( 'NONE',  #31027 ) ;
#67760=ORIENTED_EDGE ( 'NONE', *, *, #76056, .F. ) ;
#67761=ORIENTED_EDGE ( 'NONE', *, *, #125732, .F. ) ;
#67764=CARTESIAN_POINT ( 'NONE',  ( -56.99451991528749062, 28.92564299267978001, 4.000000000000000000 ) ) ;
#67765=VECTOR ( 'NONE', #56176, 1000.000000000000000 ) ;
#67768=ORIENTED_EDGE ( 'NONE', *, *, #86436, .T. ) ;
#67769=CARTESIAN_POINT ( 'NONE',  ( -26.99999999999980460, -10.06887692260771772, 4.000000000000000000 ) ) ;
#67770=DIRECTION ( 'NONE',  ( -0.000000000000000000, -0.3543493200069152693, 0.9351131265310292928 ) ) ;
#67771=EDGE_CURVE ( 'NONE', #114208, #7168, #16637, .T. ) ;
#67773=EDGE_CURVE ( 'NONE', #60350, #117136, #105082, .T. ) ;
#67774=LINE ( 'NONE', #11896, #135195 ) ;
#67775=DIRECTION ( 'NONE',  ( 0.7071067811865486830, -0.7071067811865464625, -0.000000000000000000 ) ) ;
#67776=FACE_OUTER_BOUND ( 'NONE', #95359, .T. ) ;
#67778=AXIS2_PLACEMENT_3D ( 'NONE', #80811, #81540, #16207 ) ;
#67780=CARTESIAN_POINT ( 'NONE',  ( 33.70710678118631165, 11.25929247661560062, 5.000000000000000000 ) ) ;
#67781=DIRECTION ( 'NONE',  ( 0.6830127018922180770, -0.6830127018922204085, -0.2588190451025213501 ) ) ;
#67782=ADVANCED_FACE ( 'NONE', ( #92773 ), #137009, .F. ) ;
#67783=LINE ( 'NONE', #13324, #54038 ) ;
#67784=DIRECTION ( 'NONE',  ( -4.681814790819591790E-17, -0.3543493200069152693, 0.9351131265310292928 ) ) ;
#67786=ORIENTED_EDGE ( 'NONE', *, *, #27193, .F. ) ;
#67789=CARTESIAN_POINT ( 'NONE',  ( 21.29974487139158512, -27.71228299555221142, 4.000000000000000000 ) ) ;
#67790=EDGE_CURVE ( 'NONE', #6272, #2363, #65903, .T. ) ;
#67792=ORIENTED_EDGE ( 'NONE', *, *, #100153, .T. ) ;
#67793=AXIS2_PLACEMENT_3D ( 'NONE', #68306, #55986, #100185 ) ;
#67794=DIRECTION ( 'NONE',  ( -0.7071067811865486830, -0.7071067811865464625, 0.000000000000000000 ) ) ;
#67795=DIRECTION ( 'NONE',  ( -1.000000000000000000, 0.000000000000000000, 0.000000000000000000 ) ) ;
#67796=DIRECTION ( 'NONE',  ( 0.3543493200069162685, -0.000000000000000000, -0.9351131265310288487 ) ) ;
#67797=ORIENTED_EDGE ( 'NONE', *, *, #127986, .T. ) ;
#67798=DIRECTION ( 'NONE',  ( -0.000000000000000000, -0.3543493200069152693, 0.9351131265310292928 ) ) ;
#67799=CARTESIAN_POINT ( 'NONE',  ( 3.792893218813427669, 9.759292476615620160, 5.000000000000000000 ) ) ;
#67802=VECTOR ( 'NONE', #127982, 1000.000000000000227 ) ;
#67803=DIRECTION ( 'NONE',  ( -0.7071067811865486830, 0.7071067811865464625, 0.000000000000000000 ) ) ;
#67806=VECTOR ( 'NONE', #45465, 999.9999999999998863 ) ;
#67807=VERTEX_POINT ( 'NONE', #98489 ) ;
#67808=CARTESIAN_POINT ( 'NONE',  ( -5.229957205422024913, 21.73644205237998150, 5.000000000000000888 ) ) ;
#67809=EDGE_CURVE ( 'NONE', #133121, #66646, #63747, .T. ) ;
#67810=EDGE_LOOP ( 'NONE', ( #142039, #6351, #6416, #40429 ) ) ;
#67811=VECTOR ( 'NONE', #54977, 1000.000000000000000 ) ;
#67814=CARTESIAN_POINT ( 'NONE',  ( 3.489213562373097322, -27.52281430457057709, 5.000000000000000000 ) ) ;
#67815=CARTESIAN_POINT ( 'NONE',  ( 9.489213562373095101, -27.52281430457062328, 5.000000000000000000 ) ) ;
#67817=LINE ( 'NONE', #11204, #121741 ) ;
#67818=ORIENTED_EDGE ( 'NONE', *, *, #52351, .T. ) ;
#67819=ORIENTED_EDGE ( 'NONE', *, *, #96211, .F. ) ;
#67820=CARTESIAN_POINT ( 'NONE',  ( -9.793339364578404371, 21.75929247661549581, 4.998822639870701856 ) ) ;
#67823=LINE ( 'NONE', #112013, #91369 ) ;
#67824=EDGE_CURVE ( 'NONE', #142842, #24092, #55009, .T. ) ;
#67827=CARTESIAN_POINT ( 'NONE',  ( -34.82816939922328459, -20.24070752338408141, 4.000000000000000000 ) ) ;
#67829=ORIENTED_EDGE ( 'NONE', *, *, #17321, .T. ) ;
#67832=EDGE_CURVE ( 'NONE', #102967, #63922, #129680, .T. ) ;
#67833=DIRECTION ( 'NONE',  ( -0.7071067811865486830, -0.7071067811865464625, 0.000000000000000000 ) ) ;
#67834=DIRECTION ( 'NONE',  ( -0.6830127018922180770, -0.6830127018922204085, -0.2588190451025213501 ) ) ;
#67835=VECTOR ( 'NONE', #114202, 999.9999999999998863 ) ;
#67837=ORIENTED_EDGE ( 'NONE', *, *, #65365, .F. ) ;
#67838=( BOUNDED_CURVE ( )  B_SPLINE_CURVE ( 3, ( #28049, #116479, #92559, #83144 ),
 .UNSPECIFIED., .F., .F. ) 
 B_SPLINE_CURVE_WITH_KNOTS ( ( 4, 4 ),
 ( 2.779374508378133601, 4.199602562396839822 ),
 .UNSPECIFIED. ) 
 CURVE ( )  GEOMETRIC_REPRESENTATION_ITEM ( )  RATIONAL_B_SPLINE_CURVE ( ( 1.000000000000000000, 0.8388583629366622718, 0.8388583629366622718, 1.000000000000000000 ) ) 
 REPRESENTATION_ITEM ( '' )  );
#67839=DIRECTION ( 'NONE',  ( -0.6830127018922181881, 0.6830127018922202975, -0.2588190451025214056 ) ) ;
#67840=EDGE_CURVE ( 'NONE', #88862, #142768, #21653, .T. ) ;
#67843=ORIENTED_EDGE ( 'NONE', *, *, #123034, .T. ) ;
#67844=ORIENTED_EDGE ( 'NONE', *, *, #30200, .F. ) ;
#67845=VECTOR ( 'NONE', #30196, 1000.000000000000227 ) ;
#67846=( BOUNDED_CURVE ( )  B_SPLINE_CURVE ( 3, ( #99834, #13512, #498, #22244 ),
 .UNSPECIFIED., .F., .T. ) 
 B_SPLINE_CURVE_WITH_KNOTS ( ( 4, 4 ),
 ( 0.06988172079111462653, 0.1872541115065305961 ),
 .UNSPECIFIED. ) 
 CURVE ( )  GEOMETRIC_REPRESENTATION_ITEM ( )  RATIONAL_B_SPLINE_CURVE ( ( 1.000000000000000000, 0.9988523062762910687, 0.9988523062762910687, 1.000000000000000000 ) ) 
 REPRESENTATION_ITEM ( '' )  );
#67847=CARTESIAN_POINT ( 'NONE',  ( -12.00548008471251293, 28.92564299267929684, 4.000000000000000000 ) ) ;
#67849=LINE ( 'NONE', #103269, #64883 ) ;
#67850=ADVANCED_FACE ( 'NONE', ( #29648 ), #131127, .F. ) ;
#67851=CARTESIAN_POINT ( 'NONE',  ( -44.99451991528749772, 28.92564299267969474, 4.000000000000000000 ) ) ;
#67852=CARTESIAN_POINT ( 'NONE',  ( -32.99451991528749062, 28.92564299267960948, 4.000000000000000000 ) ) ;
#67855=DIRECTION ( 'NONE',  ( -0.7071067811865486830, -0.7071067811865464625, -0.000000000000000000 ) ) ;
#67856=VECTOR ( 'NONE', #26781, 1000.000000000000000 ) ;
#67857=CARTESIAN_POINT ( 'NONE',  ( -48.18398860626899705, 28.73617430169820608, 5.000000000000000000 ) ) ;
#67858=PLANE ( 'NONE',  #131806 ) ;
#67859=VERTEX_POINT ( 'NONE', #131846 ) ;
#67860=VERTEX_POINT ( 'NONE', #65179 ) ;
#67862=ORIENTED_EDGE ( 'NONE', *, *, #52631, .F. ) ;
#67866=DIRECTION ( 'NONE',  ( -0.000000000000000000, 0.000000000000000000, 1.000000000000000000 ) ) ;
#67868=ORIENTED_EDGE ( 'NONE', *, *, #137477, .F. ) ;
#67869=ORIENTED_EDGE ( 'NONE', *, *, #118277, .F. ) ;
#67870=VECTOR ( 'NONE', #46579, 1000.000000000000000 ) ;
#67871=CARTESIAN_POINT ( 'NONE',  ( -28.49999999999979039, 1.087461875839230707, 4.000000000000000000 ) ) ;
#67872=VECTOR ( 'NONE', #112486, 999.9999999999998863 ) ;
#67874=EDGE_LOOP ( 'NONE', ( #35786, #55615, #112917, #60912 ) ) ;
#67875=EDGE_CURVE ( 'NONE', #36751, #26060, #142714, .T. ) ;
#67877=VECTOR ( 'NONE', #5274, 1000.000000000000000 ) ;
#67879=LINE ( 'NONE', #123671, #58750 ) ;
#67880=AXIS2_PLACEMENT_3D ( 'NONE', #127711, #51582, #5879 ) ;
#67882=VERTEX_POINT ( 'NONE', #97020 ) ;
#67883=FACE_BOUND ( 'NONE', #45942, .T. ) ;
#67884=ADVANCED_FACE ( 'NONE', ( #53573 ), #75332, .T. ) ;
#67885=CARTESIAN_POINT ( 'NONE',  ( 26.99999999999982236, 20.58746187583902909, 4.000000000000000000 ) ) ;
#67886=LINE ( 'NONE', #112070, #81421 ) ;
#67888=AXIS2_PLACEMENT_3D ( 'NONE', #75470, #20336, #97929 ) ;
#67889=DIRECTION ( 'NONE',  ( -0.7071067811865486830, -0.7071067811865464625, -0.000000000000000000 ) ) ;
#67891=LINE ( 'NONE', #67137, #120632 ) ;
#67894=AXIS2_PLACEMENT_3D ( 'NONE', #109650, #110341, #90029 ) ;
#67895=ORIENTED_EDGE ( 'NONE', *, *, #6266, .F. ) ;
#67897=VERTEX_POINT ( 'NONE', #141271 ) ;
#67898=PLANE ( 'NONE',  #55886 ) ;
#67899=ORIENTED_EDGE ( 'NONE', *, *, #143015, .T. ) ;
#67900=DIRECTION ( 'NONE',  ( -0.000000000000000000, 0.000000000000000000, 1.000000000000000000 ) ) ;
#67901=EDGE_CURVE ( 'NONE', #92475, #94800, #76030, .T. ) ;
#67903=FACE_OUTER_BOUND ( 'NONE', #70241, .T. ) ;
#67904=DIRECTION ( 'NONE',  ( -0.7071067811865486830, -0.7071067811865464625, 0.000000000000000000 ) ) ;
#67905=ORIENTED_EDGE ( 'NONE', *, *, #34700, .T. ) ;
#67906=FACE_OUTER_BOUND ( 'NONE', #14032, .T. ) ;
#67907=LINE ( 'NONE', #99764, #107439 ) ;
#67910=DIRECTION ( 'NONE',  ( 0.7071067811865487940, 0.7071067811865463515, 0.000000000000000000 ) ) ;
#67911=LINE ( 'NONE', #136673, #140622 ) ;
#67913=DIRECTION ( 'NONE',  ( -0.7071067811865486830, 0.7071067811865464625, 0.000000000000000000 ) ) ;
#67914=DIRECTION ( 'NONE',  ( 0.6830127018922181881, 0.6830127018922202975, -0.2588190451025214056 ) ) ;
#67915=ORIENTED_EDGE ( 'NONE', *, *, #97716, .F. ) ;
#67916=CARTESIAN_POINT ( 'NONE',  ( -19.05000000000000071, 3.174999999999997158, 4.000000000000000000 ) ) ;
#67917=PLANE ( 'NONE',  #9425 ) ;
#67918=EDGE_LOOP ( 'NONE', ( #67818, #11816, #76088, #125619 ) ) ;
#67919=ORIENTED_EDGE ( 'NONE', *, *, #8312, .T. ) ;
#67920=VERTEX_POINT ( 'NONE', #118810 ) ;
#67922=ORIENTED_EDGE ( 'NONE', *, *, #32912, .F. ) ;
#67923=AXIS2_PLACEMENT_3D ( 'NONE', #123936, #133384, #23902 ) ;
#67924=CARTESIAN_POINT ( 'NONE',  ( 20.24139925780189841, 21.72500000000000853, 5.000000000000000000 ) ) ;
#67925=EDGE_CURVE ( 'NONE', #32412, #122448, #119498, .T. ) ;
#67926=VECTOR ( 'NONE', #54046, 1000.000000000000227 ) ;
#67929=DIRECTION ( 'NONE',  ( -0.000000000000000000, -0.3543493200069152693, 0.9351131265310292928 ) ) ;
#67930=VERTEX_POINT ( 'NONE', #40561 ) ;
#67931=EDGE_CURVE ( 'NONE', #20411, #96207, #96311, .T. ) ;
#67932=EDGE_CURVE ( 'NONE', #56401, #139347, #85455, .T. ) ;
#67933=ORIENTED_EDGE ( 'NONE', *, *, #32566, .T. ) ;
#67934=CARTESIAN_POINT ( 'NONE',  ( -9.489213562373095101, -27.52281430457062328, 5.000000000000000000 ) ) ;
#67935=AXIS2_PLACEMENT_3D ( 'NONE', #7502, #130017, #51761 ) ;
#67936=CARTESIAN_POINT ( 'NONE',  ( 34.49999999999976552, 3.054329344830917670, 4.994342998332163219 ) ) ;
#67937=ORIENTED_EDGE ( 'NONE', *, *, #89196, .F. ) ;
#67938=EDGE_CURVE ( 'NONE', #91617, #70701, #86914, .T. ) ;
#67939=CARTESIAN_POINT ( 'NONE',  ( -24.48921356237309510, -27.52281430457072631, 5.000000000000000000 ) ) ;
#67940=CARTESIAN_POINT ( 'NONE',  ( -16.49999999999987921, 16.08746187583907528, 4.000000000000000000 ) ) ;
#67941=DIRECTION ( 'NONE',  ( -0.7071067811865486830, 0.7071067811865464625, 0.000000000000000000 ) ) ;
#67942=EDGE_LOOP ( 'NONE', ( #10141, #133955, #76728, #30826 ) ) ;
#67943=DIRECTION ( 'NONE',  ( 0.3543493200069162685, -0.000000000000000000, -0.9351131265310288487 ) ) ;
#67944=EDGE_LOOP ( 'NONE', ( #36584, #24745, #55272, #122050 ) ) ;
#67945=VERTEX_POINT ( 'NONE', #19499 ) ;
#67946=EDGE_LOOP ( 'NONE', ( #77605, #107204, #121285, #143419 ) ) ;
#67947=CARTESIAN_POINT ( 'NONE',  ( 15.00548008471250228, 28.92564299267927552, 4.000000000000000000 ) ) ;
#67948=AXIS2_PLACEMENT_3D ( 'NONE', #70722, #39507, #114868 ) ;
#67949=LINE ( 'NONE', #99067, #100157 ) ;
#67950=ADVANCED_FACE ( 'NONE', ( #73892 ), #32533, .F. ) ;
#67951=DIRECTION ( 'NONE',  ( -0.3543493200069162685, -0.000000000000000000, -0.9351131265310288487 ) ) ;
#67952=CARTESIAN_POINT ( 'NONE',  ( 60.48921356237309510, -27.52281430457097500, 5.000000000000000000 ) ) ;
#67953=EDGE_CURVE ( 'NONE', #99104, #113229, #76775, .T. ) ;
#67954=CARTESIAN_POINT ( 'NONE',  ( -34.49999999999975131, -7.420205493532929353, -2.617629953481332539 ) ) ;
#67956=ORIENTED_EDGE ( 'NONE', *, *, #79764, .F. ) ;
#67957=EDGE_CURVE ( 'NONE', #117376, #3502, #63046, .T. ) ;
#67959=DIRECTION ( 'NONE',  ( -0.7071067811865487940, 0.7071067811865463515, -0.000000000000000000 ) ) ;
#67960=CARTESIAN_POINT ( 'NONE',  ( 33.18398860626899705, 28.73617430169810305, 5.000000000000000000 ) ) ;
#67961=ORIENTED_EDGE ( 'NONE', *, *, #97458, .T. ) ;
#67964=PLANE ( 'NONE',  #120466 ) ;
#67966=EDGE_CURVE ( 'NONE', #120720, #138900, #68064, .T. ) ;
#67968=DIRECTION ( 'NONE',  ( -0.7071067811865486830, -0.7071067811865464625, 0.000000000000000000 ) ) ;
#67969=CARTESIAN_POINT ( 'NONE',  ( -2.510786437626908008, -27.52281430457053446, 5.000000000000000000 ) ) ;
#67970=LINE ( 'NONE', #25839, #107975 ) ;
#67971=VECTOR ( 'NONE', #108131, 1000.000000000000000 ) ;
#67972=CARTESIAN_POINT ( 'NONE',  ( -14.99999999999989519, 4.384688058510551656, -7.090945410444718711 ) ) ;
#67974=LINE ( 'NONE', #112161, #53332 ) ;
#67975=DIRECTION ( 'NONE',  ( 0.6830127018922180770, -0.6830127018922204085, -0.2588190451025213501 ) ) ;
#67976=ORIENTED_EDGE ( 'NONE', *, *, #107516, .T. ) ;
#67977=DIRECTION ( 'NONE',  ( 0.000000000000000000, 0.000000000000000000, -1.000000000000000000 ) ) ;
#67978=ADVANCED_FACE ( 'NONE', ( #121652 ), #55721, .F. ) ;
#67979=VECTOR ( 'NONE', #82199, 1000.000000000000000 ) ;
#67980=AXIS2_PLACEMENT_3D ( 'NONE', #6202, #82398, #49060 ) ;
#67981=ORIENTED_EDGE ( 'NONE', *, *, #93868, .T. ) ;
#67984=CARTESIAN_POINT ( 'NONE',  ( -34.42500000000001137, 21.72500000000000142, 0.000000000000000000 ) ) ;
#67985=CARTESIAN_POINT ( 'NONE',  ( 11.99999999999991651, -11.35517001088071076, -1.126524801160080358 ) ) ;
#67986=ORIENTED_EDGE ( 'NONE', *, *, #76217, .F. ) ;
#67987=DIRECTION ( 'NONE',  ( 0.7071067811865486830, -0.7071067811865464625, -0.000000000000000000 ) ) ;
#67988=CARTESIAN_POINT ( 'NONE',  ( 9.183988606268997046, 28.73617430169793607, 5.000000000000000000 ) ) ;
#67991=DIRECTION ( 'NONE',  ( -0.6830127018922180770, -0.6830127018922204085, -0.2588190451025213501 ) ) ;
#67992=EDGE_LOOP ( 'NONE', ( #35058, #133222, #77415, #120869 ) ) ;
#67993=CARTESIAN_POINT ( 'NONE',  ( -4.499999999999972466, 3.653845994658382779, -4.504631822206361491 ) ) ;
#67995=AXIS2_PLACEMENT_3D ( 'NONE', #106692, #8778, #53037 ) ;
#67996=PLANE ( 'NONE',  #47613 ) ;
#67997=EDGE_CURVE ( 'NONE', #100863, #49400, #46295, .T. ) ;
#68000=VECTOR ( 'NONE', #113765, 1000.000000000000000 ) ;
#68001=CARTESIAN_POINT ( 'NONE',  ( 39.29974487139159578, -27.71228299555233576, 4.000000000000000000 ) ) ;
#68002=VERTEX_POINT ( 'NONE', #135432 ) ;
#68003=LINE ( 'NONE', #131788, #16653 ) ;
#68004=DIRECTION ( 'NONE',  ( -0.7071067811865486830, 0.7071067811865464625, 0.000000000000000000 ) ) ;
#68005=CARTESIAN_POINT ( 'NONE',  ( 27.18398860626900060, 28.73617430169806042, 5.000000000000000000 ) ) ;
#68008=DIRECTION ( 'NONE',  ( -0.000000000000000000, -0.3543493200069152693, 0.9351131265310292928 ) ) ;
#68009=LINE ( 'NONE', #112193, #94142 ) ;
#68010=ORIENTED_EDGE ( 'NONE', *, *, #39893, .F. ) ;
#68012=ORIENTED_EDGE ( 'NONE', *, *, #19378, .T. ) ;
#68013=CARTESIAN_POINT ( 'NONE',  ( -20.70025512860841133, -27.71228299555191654, 4.000000000000000000 ) ) ;
#68014=ORIENTED_EDGE ( 'NONE', *, *, #13510, .T. ) ;
#68016=EDGE_CURVE ( 'NONE', #36869, #126961, #69459, .T. ) ;
#68018=CARTESIAN_POINT ( 'NONE',  ( -1.110173228882102459, -22.22500000000000497, 4.785647885939354751 ) ) ;
#68019=CARTESIAN_POINT ( 'NONE',  ( 17.99451991528748351, 28.92564299267950645, 4.000000000000000000 ) ) ;
#68020=CARTESIAN_POINT ( 'NONE',  ( -5.700255128608413102, -27.71228299555201957, 4.000000000000000000 ) ) ;
#68022=EDGE_LOOP ( 'NONE', ( #28575, #106145, #128743, #53925 ) ) ;
#68023=CARTESIAN_POINT ( 'NONE',  ( -34.92500000000001137, 12.66246187583886318, 4.000000000000000000 ) ) ;
#68025=VECTOR ( 'NONE', #38685, 1000.000000000000000 ) ;
#68027=ORIENTED_EDGE ( 'NONE', *, *, #121811, .T. ) ;
#68028=DIRECTION ( 'NONE',  ( -0.000000000000000000, 0.3543493200069153248, 0.9351131265310292928 ) ) ;
#68029=ADVANCED_FACE ( 'NONE', ( #78184 ), #123125, .T. ) ;
#68030=PLANE ( 'NONE',  #12403 ) ;
#68031=CARTESIAN_POINT ( 'NONE',  ( -45.18398860626900415, 28.73617430169818832, 5.000000000000000000 ) ) ;
#68032=ORIENTED_EDGE ( 'NONE', *, *, #98573, .T. ) ;
#68033=DIRECTION ( 'NONE',  ( 0.7071067811865486830, -0.7071067811865464625, -0.000000000000000000 ) ) ;
#68034=PLANE ( 'NONE',  #91015 ) ;
#68037=DIRECTION ( 'NONE',  ( -0.7071067811865486830, -0.7071067811865464625, 0.000000000000000000 ) ) ;
#68038=VECTOR ( 'NONE', #85144, 1000.000000000000000 ) ;
#68039=ORIENTED_EDGE ( 'NONE', *, *, #19686, .F. ) ;
#68040=ORIENTED_EDGE ( 'NONE', *, *, #20473, .F. ) ;
#68041=ORIENTED_EDGE ( 'NONE', *, *, #137161, .T. ) ;
#68043=ORIENTED_EDGE ( 'NONE', *, *, #10444, .F. ) ;
#68044=CARTESIAN_POINT ( 'NONE',  ( 27.29974487139158512, -27.71228299555225405, 4.000000000000000000 ) ) ;
#68045=EDGE_CURVE ( 'NONE', #58958, #38790, #1295, .T. ) ;
#68046=CARTESIAN_POINT ( 'NONE',  ( 39.18398860626899705, 28.73617430169814568, 5.000000000000000000 ) ) ;
#68047=VECTOR ( 'NONE', #113608, 1000.000000000000000 ) ;
#68048=DIRECTION ( 'NONE',  ( 0.7071067811865487940, -0.7071067811865463515, 0.000000000000000000 ) ) ;
#68049=CARTESIAN_POINT ( 'NONE',  ( 10.49999999999992539, -14.70932175296476352, -11.46312253303839768 ) ) ;
#68050=ORIENTED_EDGE ( 'NONE', *, *, #98039, .F. ) ;
#68051=DIRECTION ( 'NONE',  ( -0.7071067811865486830, -0.7071067811865464625, 0.000000000000000000 ) ) ;
#68052=CARTESIAN_POINT ( 'NONE',  ( 34.92499999999998295, 16.32446447596926831, 2.764066516344042324 ) ) ;
#68053=CARTESIAN_POINT ( 'NONE',  ( 10.82816939922345512, 12.75929247661558641, 4.000000000000000000 ) ) ;
#68055=ORIENTED_EDGE ( 'NONE', *, *, #86285, .T. ) ;
#68057=EDGE_CURVE ( 'NONE', #25059, #45436, #56471, .T. ) ;
#68058=DIRECTION ( 'NONE',  ( 0.7071067811865486830, -0.7071067811865464625, -0.000000000000000000 ) ) ;
#68059=VECTOR ( 'NONE', #16335, 1000.000000000000000 ) ;
#68060=LINE ( 'NONE', #115036, #30773 ) ;
#68061=ORIENTED_EDGE ( 'NONE', *, *, #61517, .F. ) ;
#68063=EDGE_CURVE ( 'NONE', #51456, #131551, #89067, .T. ) ;
#68064=LINE ( 'NONE', #33968, #83901 ) ;
#68065=ADVANCED_FACE ( 'NONE', ( #91222 ), #102064, .T. ) ;
#68066=CARTESIAN_POINT ( 'NONE',  ( -19.49999999999986144, -7.912538124160673370, 4.000000000000000000 ) ) ;
#68067=LINE ( 'NONE', #68752, #134493 ) ;
#68068=LINE ( 'NONE', #4112, #122814 ) ;
#68069=LINE ( 'NONE', #66600, #12600 ) ;
#68070=VECTOR ( 'NONE', #9164, 1000.000000000000000 ) ;
#68071=ORIENTED_EDGE ( 'NONE', *, *, #130304, .F. ) ;
#68072=ORIENTED_EDGE ( 'NONE', *, *, #97878, .T. ) ;
#68073=CARTESIAN_POINT ( 'NONE',  ( -3.183988606268992161, 28.73617430169789699, 5.000000000000000000 ) ) ;
#68075=ORIENTED_EDGE ( 'NONE', *, *, #123252, .T. ) ;
#68076=EDGE_CURVE ( 'NONE', #12889, #78582, #12187, .T. ) ;
#68077=VECTOR ( 'NONE', #2046, 999.9999999999998863 ) ;
#68078=DIRECTION ( 'NONE',  ( 0.6830127018922180770, -0.6830127018922204085, -0.2588190451025213501 ) ) ;
#68079=VERTEX_POINT ( 'NONE', #90479 ) ;
#68080=LINE ( 'NONE', #134747, #55227 ) ;
#68081=LINE ( 'NONE', #123860, #109729 ) ;
#68083=FACE_OUTER_BOUND ( 'NONE', #142402, .T. ) ;
#68084=ORIENTED_EDGE ( 'NONE', *, *, #83609, .T. ) ;
#68085=CARTESIAN_POINT ( 'NONE',  ( -38.00492477221170873, -5.240707523384228850, 12.38332538355504653 ) ) ;
#68088=ORIENTED_EDGE ( 'NONE', *, *, #61401, .T. ) ;
#68090=ORIENTED_EDGE ( 'NONE', *, *, #21404, .F. ) ;
#68091=PLANE ( 'NONE',  #6434 ) ;
#68092=VERTEX_POINT ( 'NONE', #66593 ) ;
#68093=VERTEX_POINT ( 'NONE', #12892 ) ;
#68094=AXIS2_PLACEMENT_3D ( 'NONE', #65032, #99041, #8436 ) ;
#68095=ORIENTED_EDGE ( 'NONE', *, *, #1376, .T. ) ;
#68096=DIRECTION ( 'NONE',  ( -0.3543493200069162685, -0.000000000000000000, -0.9351131265310288487 ) ) ;
#68097=VECTOR ( 'NONE', #113233, 1000.000000000000000 ) ;
#68098=ADVANCED_FACE ( 'NONE', ( #79659 ), #1983, .F. ) ;
#68099=CARTESIAN_POINT ( 'NONE',  ( 26.20710678118635784, -11.24070752338417556, 5.000000000000000000 ) ) ;
#68100=FACE_OUTER_BOUND ( 'NONE', #108789, .T. ) ;
#68102=CARTESIAN_POINT ( 'NONE',  ( 75.48921356237309510, -27.52281430457107803, 5.000000000000000000 ) ) ;
#68103=ADVANCED_FACE ( 'NONE', ( #77485 ), #101344, .F. ) ;
#68104=LINE ( 'NONE', #103509, #15791 ) ;
#68105=CARTESIAN_POINT ( 'NONE',  ( -18.18398860626898994, 28.73617430169800002, 5.000000000000000000 ) ) ;
#68106=VECTOR ( 'NONE', #123383, 1000.000000000000227 ) ;
#68107=CARTESIAN_POINT ( 'NONE',  ( -0.4892135623730947680, -27.52281430457055578, 5.000000000000000000 ) ) ;
#68108=ADVANCED_FACE ( 'NONE', ( #588 ), #44885, .T. ) ;
#68109=ADVANCED_FACE ( 'NONE', ( #57880 ), #2738, .F. ) ;
#68113=VECTOR ( 'NONE', #29043, 1000.000000000000000 ) ;
#68114=DIRECTION ( 'NONE',  ( 1.000000000000000000, 0.000000000000000000, 0.000000000000000000 ) ) ;
#68115=VECTOR ( 'NONE', #124149, 999.9999999999998863 ) ;
#68116=ORIENTED_EDGE ( 'NONE', *, *, #132488, .F. ) ;
#68117=ORIENTED_EDGE ( 'NONE', *, *, #18276, .F. ) ;
#68119=EDGE_LOOP ( 'NONE', ( #96293, #17408, #15834, #18628 ) ) ;
#68121=DIRECTION ( 'NONE',  ( -0.7071067811865487940, 0.7071067811865463515, -0.000000000000000000 ) ) ;
#68122=FACE_OUTER_BOUND ( 'NONE', #121515, .T. ) ;
#68123=EDGE_CURVE ( 'NONE', #26660, #53545, #104166, .T. ) ;
#68124=VECTOR ( 'NONE', #108868, 1000.000000000000000 ) ;
#68125=CARTESIAN_POINT ( 'NONE',  ( 10.49999999999992539, -8.568876922607726598, 4.000000000000000000 ) ) ;
#68127=DIRECTION ( 'NONE',  ( 1.000000000000000000, 0.000000000000000000, 0.000000000000000000 ) ) ;
#68128=ORIENTED_EDGE ( 'NONE', *, *, #135572, .T. ) ;
#68129=DIRECTION ( 'NONE',  ( 0.6830127018922181881, 0.6830127018922202975, -0.2588190451025214056 ) ) ;
#68130=ORIENTED_EDGE ( 'NONE', *, *, #19857, .T. ) ;
#68131=DIRECTION ( 'NONE',  ( -0.7071067811865486830, -0.7071067811865464625, 0.000000000000000000 ) ) ;
#68132=AXIS2_PLACEMENT_3D ( 'NONE', #55765, #55050, #99216 ) ;
#68133=AXIS2_PLACEMENT_3D ( 'NONE', #17596, #6694, #71307 ) ;
#68135=EDGE_LOOP ( 'NONE', ( #30214, #93436, #137566, #136839 ) ) ;
#68137=ADVANCED_FACE ( 'NONE', ( #104912 ), #119174, .F. ) ;
#68138=CARTESIAN_POINT ( 'NONE',  ( 21.18398860626899349, 28.73617430169802134, 5.000000000000000000 ) ) ;
#68140=VERTEX_POINT ( 'NONE', #93326 ) ;
#68142=ORIENTED_EDGE ( 'NONE', *, *, #59434, .F. ) ;
#68143=LINE ( 'NONE', #21734, #93559 ) ;
#68144=CARTESIAN_POINT ( 'NONE',  ( 36.29974487139159578, -27.71228299555231445, 4.000000000000000000 ) ) ;
#68145=EDGE_CURVE ( 'NONE', #59858, #107388, #114364, .T. ) ;
#68146=DIRECTION ( 'NONE',  ( -0.6830127018922180770, -0.6830127018922204085, -0.2588190451025213501 ) ) ;
#68147=PLANE ( 'NONE',  #58914 ) ;
#68148=ORIENTED_EDGE ( 'NONE', *, *, #83883, .F. ) ;
#68149=CARTESIAN_POINT ( 'NONE',  ( -17.99451991528748351, 28.92564299267950645, 4.000000000000000000 ) ) ;
#68151=LINE ( 'NONE', #100731, #11825 ) ;
#68152=CARTESIAN_POINT ( 'NONE',  ( 48.18398860626899705, 28.73617430169820608, 5.000000000000000000 ) ) ;
#68153=EDGE_LOOP ( 'NONE', ( #31709, #8946, #50526, #125308 ) ) ;
#68155=VECTOR ( 'NONE', #46383, 1000.000000000000227 ) ;
#68156=ADVANCED_FACE ( 'NONE', ( #96677 ), #102794, .T. ) ;
#68157=DIRECTION ( 'NONE',  ( 0.7071067811865487940, 0.7071067811865463515, -0.000000000000000000 ) ) ;
#68158=ORIENTED_EDGE ( 'NONE', *, *, #96074, .F. ) ;
#68160=EDGE_LOOP ( 'NONE', ( #58120, #56737, #69565, #61835 ) ) ;
#68161=EDGE_LOOP ( 'NONE', ( #21411, #125904, #2407, #124462 ) ) ;
#68162=ADVANCED_FACE ( 'NONE', ( #3436 ), #94024, .T. ) ;
#68163=FACE_OUTER_BOUND ( 'NONE', #94257, .T. ) ;
#68164=CARTESIAN_POINT ( 'NONE',  ( -34.42500000000001137, -22.22500000000000142, 5.000000000000000000 ) ) ;
#68165=ADVANCED_FACE ( 'NONE', ( #40919 ), #136827, .F. ) ;
#68166=ORIENTED_EDGE ( 'NONE', *, *, #14273, .F. ) ;
#68170=LINE ( 'NONE', #88460, #68412 ) ;
#68171=DIRECTION ( 'NONE',  ( -0.6830127018922180770, -0.6830127018922204085, -0.2588190451025213501 ) ) ;
#68172=EDGE_CURVE ( 'NONE', #143372, #128366, #140921, .T. ) ;
#68173=CARTESIAN_POINT ( 'NONE',  ( -8.700255128608413102, -27.71228299555199825, 4.000000000000000000 ) ) ;
#68174=DIRECTION ( 'NONE',  ( -0.6830127018922180770, -0.6830127018922204085, -0.2588190451025213501 ) ) ;
#68175=DIRECTION ( 'NONE',  ( 0.6830127018922180770, -0.6830127018922204085, -0.2588190451025213501 ) ) ;
#68176=CYLINDRICAL_SURFACE ( 'NONE', #125548, 0.5000000000000004441 ) ;
#68177=CARTESIAN_POINT ( 'NONE',  ( -5.939889289559763697, -9.740707523384184441, 10.89222023123382144 ) ) ;
#68180=DIRECTION ( 'NONE',  ( -0.000000000000000000, 0.3543493200069153248, 0.9351131265310292928 ) ) ;
#68182=DIRECTION ( 'NONE',  ( 0.6830127018922180770, -0.6830127018922204085, -0.2588190451025213501 ) ) ;
#68183=ORIENTED_EDGE ( 'NONE', *, *, #99069, .F. ) ;
#68184=AXIS2_PLACEMENT_3D ( 'NONE', #82857, #27738, #142239 ) ;
#68185=ORIENTED_EDGE ( 'NONE', *, *, #138606, .T. ) ;
#68187=VERTEX_POINT ( 'NONE', #41619 ) ;
#68188=EDGE_LOOP ( 'NONE', ( #99240, #61308, #143352, #112219 ) ) ;
#68189=ORIENTED_EDGE ( 'NONE', *, *, #58485, .T. ) ;
#68190=LINE ( 'NONE', #112364, #61941 ) ;
#68191=DIRECTION ( 'NONE',  ( -0.7071067811865487940, 0.7071067811865463515, -0.000000000000000000 ) ) ;
#68192=CARTESIAN_POINT ( 'NONE',  ( 0.000000000000000000, 0.000000000000000000, 5.000000000000000000 ) ) ;
#68194=DIRECTION ( 'NONE',  ( 4.681814790819592407E-17, 0.3543493200069153248, 0.9351131265310292928 ) ) ;
#68196=FACE_OUTER_BOUND ( 'NONE', #83885, .T. ) ;
#68198=VERTEX_POINT ( 'NONE', #130073 ) ;
#68199=CARTESIAN_POINT ( 'NONE',  ( 19.27928215921719612, -2.789594763390444321, 4.000000000000000000 ) ) ;
#68200=CARTESIAN_POINT ( 'NONE',  ( 21.62762920772360786, 8.558752285115851066, 4.000000000000000000 ) ) ;
#68202=VECTOR ( 'NONE', #23277, 999.9999999999998863 ) ;
#68203=CARTESIAN_POINT ( 'NONE',  ( 11.81601139373100651, 28.73617430169779041, 5.000000000000000000 ) ) ;
#68204=CARTESIAN_POINT ( 'NONE',  ( 15.70701326429294475, -21.74070752338405654, 4.999753212805220670 ) ) ;
#68205=PLANE ( 'NONE',  #59324 ) ;
#68207=LINE ( 'NONE', #123278, #26071 ) ;
#68208=AXIS2_PLACEMENT_3D ( 'NONE', #125572, #93649, #37856 ) ;
#68209=ORIENTED_EDGE ( 'NONE', *, *, #59010, .T. ) ;
#68210=ORIENTED_EDGE ( 'NONE', *, *, #137074, .T. ) ;
#68212=ORIENTED_EDGE ( 'NONE', *, *, #70327, .F. ) ;
#68213=AXIS2_PLACEMENT_3D ( 'NONE', #127890, #40861, #61240 ) ;
#68214=EDGE_CURVE ( 'NONE', #101003, #49304, #27566, .T. ) ;
#68215=PLANE ( 'NONE',  #117235 ) ;
#68216=CARTESIAN_POINT ( 'NONE',  ( -60.18398860626900415, 28.73617430169829490, 5.000000000000000000 ) ) ;
#68217=PLANE ( 'NONE',  #106888 ) ;
#68218=LINE ( 'NONE', #81204, #134607 ) ;
#68220=VECTOR ( 'NONE', #133204, 1000.000000000000000 ) ;
#68222=ORIENTED_EDGE ( 'NONE', *, *, #133470, .T. ) ;
#68223=DIRECTION ( 'NONE',  ( -0.7071067811865486830, 0.7071067811865464625, 0.000000000000000000 ) ) ;
#68224=ORIENTED_EDGE ( 'NONE', *, *, #47396, .T. ) ;
#68225=ORIENTED_EDGE ( 'NONE', *, *, #2146, .T. ) ;
#68226=EDGE_CURVE ( 'NONE', #24063, #95958, #75000, .T. ) ;
#68227=ORIENTED_EDGE ( 'NONE', *, *, #84145, .T. ) ;
#68229=EDGE_CURVE ( 'NONE', #19139, #136292, #81775, .T. ) ;
#68230=AXIS2_PLACEMENT_3D ( 'NONE', #125494, #61681, #139244 ) ;
#68231=EDGE_CURVE ( 'NONE', #43460, #115656, #81044, .T. ) ;
#68232=AXIS2_PLACEMENT_3D ( 'NONE', #22330, #112939, #2745 ) ;
#68235=ORIENTED_EDGE ( 'NONE', *, *, #112266, .F. ) ;
#68236=EDGE_CURVE ( 'NONE', #93893, #100719, #76414, .T. ) ;
#68237=ORIENTED_EDGE ( 'NONE', *, *, #62675, .T. ) ;
#68238=CARTESIAN_POINT ( 'NONE',  ( -26.29298673570676925, -21.74070752338405299, 4.999753212805220670 ) ) ;
#68241=ORIENTED_EDGE ( 'NONE', *, *, #68724, .F. ) ;
#68243=DIRECTION ( 'NONE',  ( 0.6830127018922181881, 0.6830127018922202975, -0.2588190451025214056 ) ) ;
#68244=EDGE_CURVE ( 'NONE', #71647, #86576, #75693, .T. ) ;
#68245=CARTESIAN_POINT ( 'NONE',  ( 9.489213562373095101, -27.52281430457062328, 5.000000000000000000 ) ) ;
#68247=VERTEX_POINT ( 'NONE', #97404 ) ;
#68248=DIRECTION ( 'NONE',  ( -0.6830127018922181881, 0.6830127018922202975, -0.2588190451025214056 ) ) ;
#68249=EDGE_CURVE ( 'NONE', #104684, #10438, #22683, .T. ) ;
#68250=CARTESIAN_POINT ( 'NONE',  ( -57.18398860626899705, 28.73617430169827358, 5.000000000000000000 ) ) ;
#68251=FACE_BOUND ( 'NONE', #61689, .T. ) ;
#68252=VERTEX_POINT ( 'NONE', #89412 ) ;
#68253=LINE ( 'NONE', #57358, #117368 ) ;
#68256=FACE_OUTER_BOUND ( 'NONE', #4674, .T. ) ;
#68257=ORIENTED_EDGE ( 'NONE', *, *, #57950, .F. ) ;
#68258=LINE ( 'NONE', #34892, #29547 ) ;
#68259=ORIENTED_EDGE ( 'NONE', *, *, #64449, .T. ) ;
#68260=ADVANCED_FACE ( 'NONE', ( #32178 ), #120578, .F. ) ;
#68261=ORIENTED_EDGE ( 'NONE', *, *, #12952, .T. ) ;
#68262=ADVANCED_FACE ( 'NONE', ( #133641 ), #66250, .F. ) ;
#68263=VERTEX_POINT ( 'NONE', #55372 ) ;
#68265=ORIENTED_EDGE ( 'NONE', *, *, #11749, .T. ) ;
#68267=CARTESIAN_POINT ( 'NONE',  ( 25.17183060077629619, -20.24070752338406720, 4.000000000000000000 ) ) ;
#68269=ORIENTED_EDGE ( 'NONE', *, *, #86309, .F. ) ;
#68270=DIRECTION ( 'NONE',  ( -0.000000000000000000, -0.3543493200069152693, 0.9351131265310292928 ) ) ;
#68271=LINE ( 'NONE', #44360, #38921 ) ;
#68272=AXIS2_PLACEMENT_3D ( 'NONE', #21694, #99218, #11488 ) ;
#68273=EDGE_CURVE ( 'NONE', #143262, #138986, #111134, .T. ) ;
#68274=EDGE_CURVE ( 'NONE', #97938, #3869, #141666, .T. ) ;
#68275=LINE ( 'NONE', #55952, #133553 ) ;
#68276=LINE ( 'NONE', #134948, #97121 ) ;
#68277=CARTESIAN_POINT ( 'NONE',  ( -2.510786437626908008, -27.52281430457053446, 5.000000000000000000 ) ) ;
#68278=DIRECTION ( 'NONE',  ( -0.000000000000000000, 0.000000000000000000, 1.000000000000000000 ) ) ;
#68281=VERTEX_POINT ( 'NONE', #10404 ) ;
#68282=ORIENTED_EDGE ( 'NONE', *, *, #137466, .F. ) ;
#68283=DIRECTION ( 'NONE',  ( 0.6830127018922181881, 0.6830127018922202975, -0.2588190451025214056 ) ) ;
#68284=ORIENTED_EDGE ( 'NONE', *, *, #142207, .T. ) ;
#68285=EDGE_CURVE ( 'NONE', #85221, #112404, #87984, .T. ) ;
#68288=DIRECTION ( 'NONE',  ( 0.6830127018922180770, -0.6830127018922204085, -0.2588190451025213501 ) ) ;
#68289=EDGE_CURVE ( 'NONE', #11322, #102158, #132954, .T. ) ;
#68290=DIRECTION ( 'NONE',  ( 0.6830127018922181881, 0.6830127018922202975, -0.2588190451025214056 ) ) ;
#68291=ORIENTED_EDGE ( 'NONE', *, *, #140260, .T. ) ;
#68292=PLANE ( 'NONE',  #11580 ) ;
#68293=DIRECTION ( 'NONE',  ( -0.000000000000000000, 0.000000000000000000, 1.000000000000000000 ) ) ;
#68296=PLANE ( 'NONE',  #76285 ) ;
#68297=ORIENTED_EDGE ( 'NONE', *, *, #131134, .T. ) ;
#68299=LINE ( 'NONE', #102334, #137947 ) ;
#68300=EDGE_CURVE ( 'NONE', #66246, #96290, #33633, .T. ) ;
#68302=DIRECTION ( 'NONE',  ( 1.000000000000000000, 0.000000000000000000, 0.000000000000000000 ) ) ;
#68303=CARTESIAN_POINT ( 'NONE',  ( -20.70025512860841133, -27.71228299555191654, 4.000000000000000000 ) ) ;
#68304=ORIENTED_EDGE ( 'NONE', *, *, #42171, .T. ) ;
#68305=CYLINDRICAL_SURFACE ( 'NONE', #142195, 5.968999999999998529 ) ;
#68306=CARTESIAN_POINT ( 'NONE',  ( -54.18398860626899705, 28.73617430169825226, 5.000000000000000000 ) ) ;
#68308=CARTESIAN_POINT ( 'NONE',  ( -18.87485380690754511, -14.24070752338414181, 9.401115078912701151 ) ) ;
#68309=VERTEX_POINT ( 'NONE', #121318 ) ;
#68310=EDGE_CURVE ( 'NONE', #112531, #44739, #143078, .T. ) ;
#68311=FACE_OUTER_BOUND ( 'NONE', #134405, .T. ) ;
#68312=FACE_OUTER_BOUND ( 'NONE', #42206, .T. ) ;
#68313=ORIENTED_EDGE ( 'NONE', *, *, #44603, .T. ) ;
#68314=DIRECTION ( 'NONE',  ( 0.6830127018922181881, 0.6830127018922202975, -0.2588190451025214056 ) ) ;
#68315=VECTOR ( 'NONE', #88086, 1000.000000000000000 ) ;
#68316=LINE ( 'NONE', #92863, #69633 ) ;
#68317=PLANE ( 'NONE',  #123179 ) ;
#68320=VERTEX_POINT ( 'NONE', #19860 ) ;
#68321=CARTESIAN_POINT ( 'NONE',  ( -31.49999999999977973, -4.796895815301051691, -3.611700055028753908 ) ) ;
#68323=ORIENTED_EDGE ( 'NONE', *, *, #44212, .T. ) ;
#68324=ORIENTED_EDGE ( 'NONE', *, *, #74108, .F. ) ;
#68326=DIRECTION ( 'NONE',  ( 0.7071067811865487940, 0.7071067811865463515, 0.000000000000000000 ) ) ;
#68327=EDGE_LOOP ( 'NONE', ( #82009, #51893, #80510, #72941 ) ) ;
#68328=AXIS2_PLACEMENT_3D ( 'NONE', #132370, #100428, #362 ) ;
#68329=CARTESIAN_POINT ( 'NONE',  ( -34.92500000000001137, -20.14387692260736529, 4.000000000000000000 ) ) ;
#68330=ADVANCED_FACE ( 'NONE', ( #53960 ), #132231, .F. ) ;
#68332=FACE_OUTER_BOUND ( 'NONE', #10357, .T. ) ;
#68333=DIRECTION ( 'NONE',  ( 0.6830127018922181881, 0.6830127018922202975, -0.2588190451025214056 ) ) ;
#68334=EDGE_LOOP ( 'NONE', ( #126131, #87443, #109997, #103591 ) ) ;
#68335=EDGE_CURVE ( 'NONE', #133491, #94283, #11823, .T. ) ;
#68336=DIRECTION ( 'NONE',  ( -0.000000000000000000, -0.3543493200069152693, 0.9351131265310292928 ) ) ;
#68337=VECTOR ( 'NONE', #50680, 1000.000000000000227 ) ;
#68338=LINE ( 'NONE', #57440, #2679 ) ;
#68339=CARTESIAN_POINT ( 'NONE',  ( 24.00548008471250938, 28.92564299267921513, 4.000000000000000000 ) ) ;
#68340=DIRECTION ( 'NONE',  ( -0.7071067811865486830, 0.7071067811865464625, 0.000000000000000000 ) ) ;
#68342=CARTESIAN_POINT ( 'NONE',  ( 29.99451991528749417, 28.92564299267958816, 4.000000000000000000 ) ) ;
#68343=VERTEX_POINT ( 'NONE', #43075 ) ;
#68344=EDGE_LOOP ( 'NONE', ( #63401, #114599, #10819, #4180 ) ) ;
#68346=DIRECTION ( 'NONE',  ( 0.7071067811865487940, 0.7071067811865463515, -0.000000000000000000 ) ) ;
#68347=ORIENTED_EDGE ( 'NONE', *, *, #13487, .T. ) ;
#68348=ORIENTED_EDGE ( 'NONE', *, *, #79627, .T. ) ;
#68349=ORIENTED_EDGE ( 'NONE', *, *, #26154, .F. ) ;
#68350=LINE ( 'NONE', #57454, #66487 ) ;
#68351=CARTESIAN_POINT ( 'NONE',  ( 23.28769006033955691, -21.73547319004781642, 4.999917730833664642 ) ) ;
#68352=ORIENTED_EDGE ( 'NONE', *, *, #83986, .F. ) ;
#68354=DIRECTION ( 'NONE',  ( 0.6830127018922180770, -0.6830127018922204085, -0.2588190451025214056 ) ) ;
#68355=LINE ( 'NONE', #126264, #111127 ) ;
#68356=DIRECTION ( 'NONE',  ( -0.000000000000000000, 0.3543493200069153248, 0.9351131265310292928 ) ) ;
#68358=ORIENTED_EDGE ( 'NONE', *, *, #54815, .T. ) ;
#68359=DIRECTION ( 'NONE',  ( -0.7071067811865487940, 0.7071067811865463515, -0.000000000000000000 ) ) ;
#68360=CARTESIAN_POINT ( 'NONE',  ( -33.18398860626899705, 28.73617430169810305, 5.000000000000000000 ) ) ;
#68361=PLANE ( 'NONE',  #139891 ) ;
#68362=CARTESIAN_POINT ( 'NONE',  ( 29.20710678118634718, -2.240707523384257716, 5.000000000000000000 ) ) ;
#68363=DIRECTION ( 'NONE',  ( -0.000000000000000000, -0.3543493200069152693, 0.9351131265310292928 ) ) ;
#68364=PLANE ( 'NONE',  #97812 ) ;
#68365=DIRECTION ( 'NONE',  ( 0.6830127018922180770, -0.6830127018922204085, -0.2588190451025213501 ) ) ;
#68367=CARTESIAN_POINT ( 'NONE',  ( -36.48921356237310221, -27.52281430457080802, 5.000000000000000000 ) ) ;
#68368=CARTESIAN_POINT ( 'NONE',  ( 21.48921356237309155, -27.52281430457070499, 5.000000000000000000 ) ) ;
#68369=ORIENTED_EDGE ( 'NONE', *, *, #43, .F. ) ;
#68370=ORIENTED_EDGE ( 'NONE', *, *, #134198, .T. ) ;
#68374=VERTEX_POINT ( 'NONE', #8933 ) ;
#68376=CARTESIAN_POINT ( 'NONE',  ( 1.499999999999990896, 13.46639925780212721, 5.000000000000000000 ) ) ;
#68377=EDGE_CURVE ( 'NONE', #16488, #23262, #53201, .T. ) ;
#68379=VERTEX_POINT ( 'NONE', #13252 ) ;
#68380=DIRECTION ( 'NONE',  ( 0.7071067811865486830, -0.7071067811865464625, -0.000000000000000000 ) ) ;
#68382=CARTESIAN_POINT ( 'NONE',  ( 6.328169399223488867, -15.74070752338412049, 4.000000000000000000 ) ) ;
#68384=ADVANCED_FACE ( 'NONE', ( #15380 ), #112596, .F. ) ;
#68385=DIRECTION ( 'NONE',  ( 0.7071067811865487940, -0.7071067811865463515, 0.000000000000000000 ) ) ;
#68386=ORIENTED_EDGE ( 'NONE', *, *, #111958, .F. ) ;
#68387=DIRECTION ( 'NONE',  ( -0.6830127018922181881, 0.6830127018922202975, -0.2588190451025214056 ) ) ;
#68388=EDGE_CURVE ( 'NONE', #109916, #96830, #48776, .T. ) ;
#68390=ORIENTED_EDGE ( 'NONE', *, *, #129444, .F. ) ;
#68391=CARTESIAN_POINT ( 'NONE',  ( 33.29974487139158867, -27.71228299555229313, 4.000000000000000000 ) ) ;
#68392=LINE ( 'NONE', #112571, #124896 ) ;
#68393=CARTESIAN_POINT ( 'NONE',  ( 48.18398860626899705, 28.73617430169820608, 5.000000000000000000 ) ) ;
#68394=CARTESIAN_POINT ( 'NONE',  ( 34.92499999999998295, -16.29806943317885271, 4.500000000000000888 ) ) ;
#68395=EDGE_CURVE ( 'NONE', #28531, #120155, #67703, .T. ) ;
#68396=ADVANCED_FACE ( 'NONE', ( #137213 ), #111886, .T. ) ;
#68397=AXIS2_PLACEMENT_3D ( 'NONE', #67276, #1263, #86881 ) ;
#68398=ORIENTED_EDGE ( 'NONE', *, *, #71263, .T. ) ;
#68400=CARTESIAN_POINT ( 'NONE',  ( -26.29289321881326913, -6.740707523384207533, 5.000000000000000000 ) ) ;
#68402=VECTOR ( 'NONE', #10695, 999.9999999999998863 ) ;
#68403=CARTESIAN_POINT ( 'NONE',  ( 27.32816939922334143, 8.259292476615632594, 4.000000000000000000 ) ) ;
#68404=EDGE_CURVE ( 'NONE', #20953, #123646, #37910, .T. ) ;
#68405=CARTESIAN_POINT ( 'NONE',  ( 18.29974487139159223, -27.71228299555219010, 4.000000000000000000 ) ) ;
#68406=CARTESIAN_POINT ( 'NONE',  ( -7.499999999999944045, -16.53360074219757081, 5.000000000000000000 ) ) ;
#68407=ORIENTED_EDGE ( 'NONE', *, *, #52942, .F. ) ;
#68408=VERTEX_POINT ( 'NONE', #135776 ) ;
#68409=DIRECTION ( 'NONE',  ( -0.7071067811865486830, 0.7071067811865464625, 0.000000000000000000 ) ) ;
#68410=VERTEX_POINT ( 'NONE', #124895 ) ;
#68411=EDGE_CURVE ( 'NONE', #94185, #30378, #32255, .T. ) ;
#68412=VECTOR ( 'NONE', #80441, 1000.000000000000000 ) ;
#68413=CARTESIAN_POINT ( 'NONE',  ( -39.88837638105217565, 9.759292476615614831, 17.35367589129221955 ) ) ;
#68414=VERTEX_POINT ( 'NONE', #136473 ) ;
#68416=DIRECTION ( 'NONE',  ( -0.000000000000000000, -0.3543493200069152693, 0.9351131265310292928 ) ) ;
#68417=CARTESIAN_POINT ( 'NONE',  ( 36.29974487139159578, -27.71228299555231445, 4.000000000000000000 ) ) ;
#68418=FACE_BOUND ( 'NONE', #98000, .T. ) ;
#68419=CARTESIAN_POINT ( 'NONE',  ( -34.92500000000001137, 22.22500000000000142, 4.000000000000000000 ) ) ;
#68421=CARTESIAN_POINT ( 'NONE',  ( 54.29974487139159578, -27.71228299555243879, 4.000000000000000000 ) ) ;
#68422=CARTESIAN_POINT ( 'NONE',  ( 0.000000000000000000, 0.000000000000000000, 5.000000000000000000 ) ) ;
#68423=DIRECTION ( 'NONE',  ( -0.000000000000000000, -0.3543493200069152693, 0.9351131265310292928 ) ) ;
#68424=VERTEX_POINT ( 'NONE', #46682 ) ;
#68425=ADVANCED_FACE ( 'NONE', ( #26305 ), #13964, .T. ) ;
#68426=DIRECTION ( 'NONE',  ( 1.000000000000000000, 0.000000000000000000, 0.000000000000000000 ) ) ;
#68428=ORIENTED_EDGE ( 'NONE', *, *, #116149, .T. ) ;
#68429=VECTOR ( 'NONE', #56262, 1000.000000000000000 ) ;
#68430=ORIENTED_EDGE ( 'NONE', *, *, #11576, .T. ) ;
#68432=ORIENTED_EDGE ( 'NONE', *, *, #137577, .T. ) ;
#68433=AXIS2_PLACEMENT_3D ( 'NONE', #89238, #33464, #79112 ) ;
#68434=DIRECTION ( 'NONE',  ( -0.7071067811865486830, -0.7071067811865464625, 0.000000000000000000 ) ) ;
#68436=ORIENTED_EDGE ( 'NONE', *, *, #40975, .F. ) ;
#68437=DIRECTION ( 'NONE',  ( 0.7071067811865487940, -0.7071067811865463515, 0.000000000000000000 ) ) ;
#68438=DIRECTION ( 'NONE',  ( -0.7071067811865487940, 0.7071067811865463515, 0.000000000000000000 ) ) ;
#68439=ADVANCED_FACE ( 'NONE', ( #14706 ), #103140, .T. ) ;
#68440=LINE ( 'NONE', #12578, #105775 ) ;
#68441=CARTESIAN_POINT ( 'NONE',  ( -34.45011844616453800, 10.51628081163737249, 5.000000000000000888 ) ) ;
#68442=CARTESIAN_POINT ( 'NONE',  ( -26.99999999999981526, -10.77435723561697145, -9.972017380717165480 ) ) ;
#68443=DIRECTION ( 'NONE',  ( 0.6830127018922180770, -0.6830127018922204085, -0.2588190451025213501 ) ) ;
#68444=EDGE_CURVE ( 'NONE', #97623, #53287, #123504, .T. ) ;
#68445=CARTESIAN_POINT ( 'NONE',  ( -8.207106781186489286, 3.759292476615680112, 5.000000000000000000 ) ) ;
#68447=VERTEX_POINT ( 'NONE', #1647 ) ;
#68448=EDGE_LOOP ( 'NONE', ( #87851, #105696, #56259, #76621 ) ) ;
#68449=LINE ( 'NONE', #45271, #21879 ) ;
#68451=EDGE_LOOP ( 'NONE', ( #79511, #33125, #126041 ) ) ;
#68452=ADVANCED_FACE ( 'NONE', ( #134361 ), #102456, .T. ) ;
#68453=ORIENTED_EDGE ( 'NONE', *, *, #124168, .T. ) ;
#68454=ORIENTED_EDGE ( 'NONE', *, *, #123365, .T. ) ;
#68456=VERTEX_POINT ( 'NONE', #37170 ) ;
#68457=PLANE ( 'NONE',  #83340 ) ;
#68459=CARTESIAN_POINT ( 'NONE',  ( -2.999999999999975131, 12.83542986846996925, -1.025386466790363826 ) ) ;
#68461=PLANE ( 'NONE',  #44992 ) ;
#68463=EDGE_CURVE ( 'NONE', #15691, #109971, #114708, .T. ) ;
#68464=FACE_OUTER_BOUND ( 'NONE', #112864, .T. ) ;
#68465=CARTESIAN_POINT ( 'NONE',  ( 9.005480084712511157, 28.92564299267931816, 4.000000000000000000 ) ) ;
#68466=CARTESIAN_POINT ( 'NONE',  ( 0.7071067811865432429, 8.259292476615634371, 5.000000000000000000 ) ) ;
#68468=VERTEX_POINT ( 'NONE', #50912 ) ;
#68469=ORIENTED_EDGE ( 'NONE', *, *, #29725, .T. ) ;
#68470=LINE ( 'NONE', #122081, #98203 ) ;
#68471=DIRECTION ( 'NONE',  ( 0.7071067811865486830, -0.7071067811865464625, -0.000000000000000000 ) ) ;
#68472=DIRECTION ( 'NONE',  ( -0.000000000000000000, 0.3543493200069153248, 0.9351131265310292928 ) ) ;
#68473=ORIENTED_EDGE ( 'NONE', *, *, #44476, .F. ) ;
#68474=FACE_OUTER_BOUND ( 'NONE', #19491, .T. ) ;
#68475=DIRECTION ( 'NONE',  ( 0.6830127018922180770, -0.6830127018922204085, -0.2588190451025213501 ) ) ;
#68477=CARTESIAN_POINT ( 'NONE',  ( -28.82816939922332367, 15.75929247661555443, 4.000000000000000000 ) ) ;
#68478=CARTESIAN_POINT ( 'NONE',  ( -34.49999999999976552, 0.05432934483094037370, 4.994342998332168548 ) ) ;
#68479=DIRECTION ( 'NONE',  ( -0.7071067811865486830, 0.7071067811865464625, 0.000000000000000000 ) ) ;
#68484=EDGE_CURVE ( 'NONE', #56571, #118999, #40751, .T. ) ;
#68489=VECTOR ( 'NONE', #48926, 1000.000000000000000 ) ;
#68490=DIRECTION ( 'NONE',  ( 0.7071067811865486830, -0.7071067811865464625, -0.000000000000000000 ) ) ;
#68491=EDGE_CURVE ( 'NONE', #34745, #138332, #41541, .T. ) ;
#68493=DIRECTION ( 'NONE',  ( -0.000000000000000000, 0.000000000000000000, 1.000000000000000000 ) ) ;
#68494=DIRECTION ( 'NONE',  ( 0.7071067811865486830, -0.7071067811865464625, -0.000000000000000000 ) ) ;
#68495=LINE ( 'NONE', #55454, #86144 ) ;
#68497=ORIENTED_EDGE ( 'NONE', *, *, #81411, .F. ) ;
#68498=CARTESIAN_POINT ( 'NONE',  ( -14.99999999999988098, 20.58746187583902554, 4.000000000000000000 ) ) ;
#68499=PLANE ( 'NONE',  #123340 ) ;
#68500=CARTESIAN_POINT ( 'NONE',  ( 1.147419327679491285, 22.22500000000000142, 18.66918814110288238 ) ) ;
#68502=CARTESIAN_POINT ( 'NONE',  ( -19.43312800248730099, -21.74070752338405654, 6.915939825044120859 ) ) ;
#68503=EDGE_CURVE ( 'NONE', #70270, #36313, #140746, .T. ) ;
#68504=CARTESIAN_POINT ( 'NONE',  ( -34.92500000000001137, 19.70193056682081334, 4.500000000000000888 ) ) ;
#68505=DIRECTION ( 'NONE',  ( 0.7071067811865487940, 0.7071067811865463515, 0.000000000000000000 ) ) ;
#68506=ORIENTED_EDGE ( 'NONE', *, *, #133712, .T. ) ;
#68507=DIRECTION ( 'NONE',  ( -0.6830127018922180770, -0.6830127018922204085, -0.2588190451025213501 ) ) ;
#68508=ORIENTED_EDGE ( 'NONE', *, *, #49747, .F. ) ;
#68511=LINE ( 'NONE', #122860, #92868 ) ;
#68513=EDGE_CURVE ( 'NONE', #103695, #75761, #74088, .T. ) ;
#68514=PLANE ( 'NONE',  #9294 ) ;
#68515=LINE ( 'NONE', #33744, #131082 ) ;
#68518=CARTESIAN_POINT ( 'NONE',  ( -9.183988606268997046, 28.73617430169793607, 5.000000000000000000 ) ) ;
#68521=AXIS2_PLACEMENT_3D ( 'NONE', #1783, #46085, #90261 ) ;
#68522=CARTESIAN_POINT ( 'NONE',  ( 31.03163515922171811, 2.259292476615690770, 13.77329220150644673 ) ) ;
#68524=DIRECTION ( 'NONE',  ( -0.3543493200069162685, -0.000000000000000000, -0.9351131265310288487 ) ) ;
#68526=DIRECTION ( 'NONE',  ( -0.000000000000000000, 0.3543493200069153248, 0.9351131265310292928 ) ) ;
#68527=VERTEX_POINT ( 'NONE', #139379 ) ;
#68530=PLANE ( 'NONE',  #5255 ) ;
#68531=LINE ( 'NONE', #90991, #9157 ) ;
#68532=CARTESIAN_POINT ( 'NONE',  ( 17.81601139373099940, 28.73617430169775133, 5.000000000000000000 ) ) ;
#68533=VECTOR ( 'NONE', #39784, 999.9999999999998863 ) ;
#68534=VERTEX_POINT ( 'NONE', #105964 ) ;
#68535=LINE ( 'NONE', #46812, #86159 ) ;
#68539=VERTEX_POINT ( 'NONE', #27003 ) ;
#68541=CARTESIAN_POINT ( 'NONE',  ( -42.29974487139158157, -27.71228299555235708, 4.000000000000000000 ) ) ;
#68542=DIRECTION ( 'NONE',  ( 0.7071067811865487940, 0.7071067811865463515, -0.000000000000000000 ) ) ;
#68543=FACE_OUTER_BOUND ( 'NONE', #80369, .T. ) ;
#68544=EDGE_CURVE ( 'NONE', #97146, #18696, #117552, .T. ) ;
#68547=CARTESIAN_POINT ( 'NONE',  ( -12.18398860626900060, 28.73617430169795739, 5.000000000000000000 ) ) ;
#68548=DIRECTION ( 'NONE',  ( 0.7071067811865487940, 0.7071067811865463515, -0.000000000000000000 ) ) ;
#68549=DIRECTION ( 'NONE',  ( 1.000000000000000000, 0.000000000000000000, 0.000000000000000000 ) ) ;
#68550=CARTESIAN_POINT ( 'NONE',  ( 25.21321903303343248, 12.75929247661558641, 10.29404684609041176 ) ) ;
#68551=ORIENTED_EDGE ( 'NONE', *, *, #94255, .T. ) ;
#68552=EDGE_CURVE ( 'NONE', #66092, #81560, #5230, .T. ) ;
#68553=VERTEX_POINT ( 'NONE', #93701 ) ;
#68554=EDGE_CURVE ( 'NONE', #88238, #79108, #137926, .T. ) ;
#68557=ADVANCED_FACE ( 'NONE', ( #35 ), #11638, .F. ) ;
#68558=CARTESIAN_POINT ( 'NONE',  ( -9.792893218813388145, 6.759292476615645029, 5.000000000000000000 ) ) ;
#68559=CARTESIAN_POINT ( 'NONE',  ( 6.183988606268994381, 28.73617430169791476, 5.000000000000000000 ) ) ;
#68560=CARTESIAN_POINT ( 'NONE',  ( 8.700255128608413102, -27.71228299555199825, 4.000000000000000000 ) ) ;
#68562=PLANE ( 'NONE',  #48034 ) ;
#68563=PLANE ( 'NONE',  #119561 ) ;
#68564=ORIENTED_EDGE ( 'NONE', *, *, #79867, .T. ) ;
#68565=ORIENTED_EDGE ( 'NONE', *, *, #110779, .T. ) ;
#68566=EDGE_CURVE ( 'NONE', #34037, #142123, #31301, .T. ) ;
#68569=EDGE_CURVE ( 'NONE', #106062, #133913, #42903, .T. ) ;
#68572=LINE ( 'NONE', #25021, #111890 ) ;
#68573=ORIENTED_EDGE ( 'NONE', *, *, #126311, .F. ) ;
#68574=EDGE_CURVE ( 'NONE', #120179, #130843, #77666, .T. ) ;
#68575=FACE_BOUND ( 'NONE', #6893, .T. ) ;
#68576=CARTESIAN_POINT ( 'NONE',  ( -8.994519915287490619, 28.92564299267944250, 4.000000000000000000 ) ) ;
#68577=PLANE ( 'NONE',  #326 ) ;
#68578=CARTESIAN_POINT ( 'NONE',  ( 14.14818355038136133, 17.25929247661554555, 8.802941693769234632 ) ) ;
#68579=CARTESIAN_POINT ( 'NONE',  ( -81.29974487139159578, -27.71228299555262709, 4.000000000000000000 ) ) ;
#68581=PLANE ( 'NONE',  #76715 ) ;
#68584=VERTEX_POINT ( 'NONE', #63928 ) ;
#68587=VERTEX_POINT ( 'NONE', #121137 ) ;
#68588=VECTOR ( 'NONE', #17359, 999.9999999999998863 ) ;
#68590=VERTEX_POINT ( 'NONE', #55918 ) ;
#68592=DIRECTION ( 'NONE',  ( 0.7071067811865486830, -0.7071067811865464625, -0.000000000000000000 ) ) ;
#68593=ORIENTED_EDGE ( 'NONE', *, *, #89475, .T. ) ;
#68594=LINE ( 'NONE', #35263, #6628 ) ;
#68596=AXIS2_PLACEMENT_3D ( 'NONE', #18341, #9620, #141599 ) ;
#68597=LINE ( 'NONE', #122960, #87464 ) ;
#68598=CARTESIAN_POINT ( 'NONE',  ( -0.4981634851395633223, -17.24070752338410628, 8.407044977365226046 ) ) ;
#68599=ADVANCED_FACE ( 'NONE', ( #55194 ), #33467, .F. ) ;
#68600=LINE ( 'NONE', #135971, #53129 ) ;
#68601=CARTESIAN_POINT ( 'NONE',  ( 7.499999999999958256, 4.466399257802219580, 5.000000000000000000 ) ) ;
#68602=EDGE_LOOP ( 'NONE', ( #120429, #5929, #71462, #20552 ) ) ;
#68603=DIRECTION ( 'NONE',  ( -0.7071067811865486830, -0.7071067811865464625, 0.000000000000000000 ) ) ;
#68604=EDGE_CURVE ( 'NONE', #81804, #127735, #44333, .T. ) ;
#68605=CARTESIAN_POINT ( 'NONE',  ( 26.99999999999981526, -15.03360074219758147, 5.000000000000000000 ) ) ;
#68606=ORIENTED_EDGE ( 'NONE', *, *, #103705, .F. ) ;
#68607=VECTOR ( 'NONE', #60903, 1000.000000000000000 ) ;
#68608=EDGE_LOOP ( 'NONE', ( #134333, #133653, #64899, #111688 ) ) ;
#68609=VERTEX_POINT ( 'NONE', #108813 ) ;
#68611=EDGE_LOOP ( 'NONE', ( #95757, #117088, #68349, #15336 ) ) ;
#68612=EDGE_CURVE ( 'NONE', #109110, #138595, #66080, .T. ) ;
#68613=VECTOR ( 'NONE', #16069, 999.9999999999998863 ) ;
#68615=CARTESIAN_POINT ( 'NONE',  ( -39.29974487139159578, -27.71228299555233576, 4.000000000000000000 ) ) ;
#68616=AXIS2_PLACEMENT_3D ( 'NONE', #7854, #17317, #49276 ) ;
#68619=DIRECTION ( 'NONE',  ( 0.7071067811865486830, -0.7071067811865464625, -0.000000000000000000 ) ) ;
#68621=VECTOR ( 'NONE', #134139, 1000.000000000000000 ) ;
#68622=EDGE_CURVE ( 'NONE', #139225, #124741, #110244, .T. ) ;
#68623=LINE ( 'NONE', #25068, #84968 ) ;
#68625=DIRECTION ( 'NONE',  ( 0.7071067811865487940, 0.7071067811865463515, 0.000000000000000000 ) ) ;
#68626=VECTOR ( 'NONE', #64558, 1000.000000000000114 ) ;
#68627=DIRECTION ( 'NONE',  ( 0.7071067811865487940, 0.7071067811865463515, 0.000000000000000000 ) ) ;
#68628=EDGE_LOOP ( 'NONE', ( #31511, #23254, #14971, #40193 ) ) ;
#68630=DIRECTION ( 'NONE',  ( -0.000000000000000000, 0.3543493200069153248, 0.9351131265310292928 ) ) ;
#68632=ORIENTED_EDGE ( 'NONE', *, *, #58313, .F. ) ;
#68633=CARTESIAN_POINT ( 'NONE',  ( 5.671830600776432973, -9.740707523384186217, 4.000000000000000000 ) ) ;
#68634=ORIENTED_EDGE ( 'NONE', *, *, #107140, .T. ) ;
#68635=ORIENTED_EDGE ( 'NONE', *, *, #11756, .T. ) ;
#68636=ORIENTED_EDGE ( 'NONE', *, *, #36440, .T. ) ;
#68638=CARTESIAN_POINT ( 'NONE',  ( -33.29974487139158867, -27.71228299555229313, 4.000000000000000000 ) ) ;
#68639=DIRECTION ( 'NONE',  ( -0.000000000000000000, -0.3543493200069152693, 0.9351131265310292928 ) ) ;
#68640=EDGE_CURVE ( 'NONE', #89124, #56014, #88546, .T. ) ;
#68641=DIRECTION ( 'NONE',  ( -0.7071067811865487940, 0.7071067811865463515, -0.000000000000000000 ) ) ;
#68642=DIRECTION ( 'NONE',  ( 0.7071067811865487940, -0.7071067811865463515, 0.000000000000000000 ) ) ;
#68643=EDGE_LOOP ( 'NONE', ( #139001, #127308, #134849, #89562 ) ) ;
#68646=CARTESIAN_POINT ( 'NONE',  ( 3.604862331875187564, 21.75929247661549937, 21.32995629748186062 ) ) ;
#68647=VECTOR ( 'NONE', #106364, 999.9999999999998863 ) ;
#68648=LINE ( 'NONE', #112832, #64531 ) ;
#68650=ORIENTED_EDGE ( 'NONE', *, *, #84357, .T. ) ;
#68651=ORIENTED_EDGE ( 'NONE', *, *, #126628, .T. ) ;
#68652=VERTEX_POINT ( 'NONE', #132780 ) ;
#68653=CARTESIAN_POINT ( 'NONE',  ( 39.18398860626899705, 28.73617430169814568, 5.000000000000000000 ) ) ;
#68654=DIRECTION ( 'NONE',  ( 0.6830127018922181881, 0.6830127018922202975, -0.2588190451025214056 ) ) ;
#68655=VECTOR ( 'NONE', #125589, 1000.000000000000000 ) ;
#68656=PLANE ( 'NONE',  #91376 ) ;
#68657=CARTESIAN_POINT ( 'NONE',  ( 34.42499999999998295, -12.02281430457047939, 5.000000000000000000 ) ) ;
#68659=( BOUNDED_CURVE ( )  B_SPLINE_CURVE ( 3, ( #124234, #23486, #136521, #69158 ),
 .UNSPECIFIED., .F., .F. ) 
 B_SPLINE_CURVE_WITH_KNOTS ( ( 4, 4 ),
 ( 2.605825008650064500, 2.701628967222373223 ),
 .UNSPECIFIED. ) 
 CURVE ( )  GEOMETRIC_REPRESENTATION_ITEM ( )  RATIONAL_B_SPLINE_CURVE ( ( 1.000000000000000000, 0.9992352797041761381, 0.9992352797041761381, 1.000000000000000000 ) ) 
 REPRESENTATION_ITEM ( '' )  );
#68660=EDGE_CURVE ( 'NONE', #92375, #50477, #2584, .T. ) ;
#68661=PLANE ( 'NONE',  #103966 ) ;
#68663=LINE ( 'NONE', #132511, #96497 ) ;
#68664=CARTESIAN_POINT ( 'NONE',  ( 20.99999999999985789, 8.966399257802171618, 5.000000000000000000 ) ) ;
#68666=DIRECTION ( 'NONE',  ( 1.000000000000000000, 0.000000000000000000, 0.000000000000000000 ) ) ;
#68667=VECTOR ( 'NONE', #98261, 1000.000000000000000 ) ;
#68668=ORIENTED_EDGE ( 'NONE', *, *, #40066, .T. ) ;
#68669=CARTESIAN_POINT ( 'NONE',  ( 18.18398860626898994, 28.73617430169800002, 5.000000000000000000 ) ) ;
#68670=EDGE_LOOP ( 'NONE', ( #78166, #114395, #139299, #118616 ) ) ;
#68671=( BOUNDED_CURVE ( )  B_SPLINE_CURVE ( 3, ( #77535, #121699, #20243, #131169 ),
 .UNSPECIFIED., .F., .T. ) 
 B_SPLINE_CURVE_WITH_KNOTS ( ( 4, 4 ),
 ( 1.989451877885351383, 2.205626217416131407 ),
 .UNSPECIFIED. ) 
 CURVE ( )  GEOMETRIC_REPRESENTATION_ITEM ( )  RATIONAL_B_SPLINE_CURVE ( ( 1.000000000000000000, 0.9961095111196431873, 0.9961095111196431873, 1.000000000000000000 ) ) 
 REPRESENTATION_ITEM ( '' )  );
#68672=DIRECTION ( 'NONE',  ( -0.7071067811865486830, 0.7071067811865464625, 0.000000000000000000 ) ) ;
#68673=ORIENTED_EDGE ( 'NONE', *, *, #24159, .F. ) ;
#68676=CARTESIAN_POINT ( 'NONE',  ( -57.29974487139158157, -27.71228299555246011, 4.000000000000000000 ) ) ;
#68677=ORIENTED_EDGE ( 'NONE', *, *, #94380, .F. ) ;
#68678=CARTESIAN_POINT ( 'NONE',  ( -72.18398860626899705, 28.73617430169837661, 5.000000000000000000 ) ) ;
#68679=ORIENTED_EDGE ( 'NONE', *, *, #142085, .T. ) ;
#68681=VERTEX_POINT ( 'NONE', #10925 ) ;
#68682=CARTESIAN_POINT ( 'NONE',  ( -22.82816939922337696, -11.24070752338416490, 4.000000000000000000 ) ) ;
#68685=CARTESIAN_POINT ( 'NONE',  ( 32.99999999999977263, -8.151047557385043163, -8.977947279169878669 ) ) ;
#68688=VECTOR ( 'NONE', #88353, 1000.000000000000000 ) ;
#68690=CARTESIAN_POINT ( 'NONE',  ( -32.67183060077624646, -12.74070752338415424, 4.000000000000000000 ) ) ;
#68692=CARTESIAN_POINT ( 'NONE',  ( -60.48921356237309510, -27.52281430457097500, 5.000000000000000000 ) ) ;
#68694=DIRECTION ( 'NONE',  ( -0.7071067811865486830, -0.7071067811865464625, 0.000000000000000000 ) ) ;
#68695=ORIENTED_EDGE ( 'NONE', *, *, #117930, .F. ) ;
#68696=DIRECTION ( 'NONE',  ( -0.7071067811865486830, -0.7071067811865464625, 0.000000000000000000 ) ) ;
#68700=DIRECTION ( 'NONE',  ( -0.7071067811865486830, -0.7071067811865464625, 0.000000000000000000 ) ) ;
#68701=LINE ( 'NONE', #68019, #134317 ) ;
#68702=DIRECTION ( 'NONE',  ( -0.000000000000000000, -0.3543493200069152693, 0.9351131265310292928 ) ) ;
#68704=CARTESIAN_POINT ( 'NONE',  ( 8.671830600776408104, 20.25929247661551713, 4.000000000000000000 ) ) ;
#68705=CARTESIAN_POINT ( 'NONE',  ( -9.706792507240685097, 20.25929247661552068, 20.83292124670817103 ) ) ;
#68706=DIRECTION ( 'NONE',  ( 0.7071067811865487940, -0.7071067811865463515, 0.000000000000000000 ) ) ;
#68707=AXIS2_PLACEMENT_3D ( 'NONE', #77135, #74989, #43065 ) ;
#68708=ORIENTED_EDGE ( 'NONE', *, *, #112878, .T. ) ;
#68709=CARTESIAN_POINT ( 'NONE',  ( 24.70057660522904897, 5.105512181938189897, 4.576947331497495774 ) ) ;
#68710=CARTESIAN_POINT ( 'NONE',  ( 19.05000000000000071, 3.174999999999997158, 5.000000000000000000 ) ) ;
#68711=CARTESIAN_POINT ( 'NONE',  ( -34.92500000000001137, -1.298069433178978382, 4.500000000000000888 ) ) ;
#68712=ORIENTED_EDGE ( 'NONE', *, *, #49062, .T. ) ;
#68714=DIRECTION ( 'NONE',  ( -0.7071067811865487940, 0.7071067811865463515, 0.000000000000000000 ) ) ;
#68716=PLANE ( 'NONE',  #91873 ) ;
#68717=VECTOR ( 'NONE', #19329, 1000.000000000000000 ) ;
#68719=VECTOR ( 'NONE', #29658, 1000.000000000000000 ) ;
#68720=VERTEX_POINT ( 'NONE', #108100 ) ;
#68721=ORIENTED_EDGE ( 'NONE', *, *, #9052, .F. ) ;
#68722=ORIENTED_EDGE ( 'NONE', *, *, #22162, .F. ) ;
#68724=EDGE_CURVE ( 'NONE', #38512, #1490, #119006, .T. ) ;
#68726=VERTEX_POINT ( 'NONE', #97218 ) ;
#68727=ADVANCED_FACE ( 'NONE', ( #142215 ), #64629, .F. ) ;
#68728=ADVANCED_FACE ( 'NONE', ( #112422 ), #25385, .T. ) ;
#68730=CARTESIAN_POINT ( 'NONE',  ( -34.92500000000001137, 10.70193056682090749, 4.500000000000000888 ) ) ;
#68731=EDGE_CURVE ( 'NONE', #41471, #86576, #133466, .T. ) ;
#68733=AXIS2_PLACEMENT_3D ( 'NONE', #123248, #68182, #101460 ) ;
#68734=LINE ( 'NONE', #37524, #100967 ) ;
#68735=ORIENTED_EDGE ( 'NONE', *, *, #121360, .T. ) ;
#68736=ADVANCED_FACE ( 'NONE', ( #124016 ), #100824, .F. ) ;
#68737=DIRECTION ( 'NONE',  ( -0.000000000000000000, 0.3543493200069152138, -0.9351131265310292928 ) ) ;
#68738=FACE_OUTER_BOUND ( 'NONE', #92150, .T. ) ;
#68741=ORIENTED_EDGE ( 'NONE', *, *, #72003, .F. ) ;
#68742=ADVANCED_FACE ( 'NONE', ( #57352 ), #15212, .F. ) ;
#68744=LINE ( 'NONE', #102790, #44667 ) ;
#68746=ORIENTED_EDGE ( 'NONE', *, *, #138255, .F. ) ;
#68747=ADVANCED_FACE ( 'NONE', ( #34155 ), #773, .F. ) ;
#68748=DIRECTION ( 'NONE',  ( 1.000000000000000000, 0.000000000000000000, 0.000000000000000000 ) ) ;
#68749=ADVANCED_FACE ( 'NONE', ( #134178 ), #111707, .T. ) ;
#68752=CARTESIAN_POINT ( 'NONE',  ( 24.18398860626899705, 28.73617430169804265, 5.000000000000000000 ) ) ;
#68753=CARTESIAN_POINT ( 'NONE',  ( -18.18398860626898994, 28.73617430169800002, 5.000000000000000000 ) ) ;
#68754=EDGE_CURVE ( 'NONE', #92427, #114903, #3613, .T. ) ;
#68755=PLANE ( 'NONE',  #18679 ) ;
#68758=VECTOR ( 'NONE', #75233, 1000.000000000000227 ) ;
#68759=ORIENTED_EDGE ( 'NONE', *, *, #7980, .F. ) ;
#68760=ORIENTED_EDGE ( 'NONE', *, *, #83055, .T. ) ;
#68761=CARTESIAN_POINT ( 'NONE',  ( -6.707106781186496391, 14.25929247661557575, 5.000000000000000000 ) ) ;
#68762=EDGE_LOOP ( 'NONE', ( #89848, #41786, #12424, #8347 ) ) ;
#68763=ORIENTED_EDGE ( 'NONE', *, *, #68310, .T. ) ;
#68764=AXIS2_PLACEMENT_3D ( 'NONE', #40713, #16048, #92937 ) ;
#68765=DIRECTION ( 'NONE',  ( -0.7071067811865487940, 0.7071067811865463515, 0.000000000000000000 ) ) ;
#68766=ORIENTED_EDGE ( 'NONE', *, *, #132412, .F. ) ;
#68770=CARTESIAN_POINT ( 'NONE',  ( 25.58990935480152729, 9.759292476615618384, 11.28811694763784779 ) ) ;
#68771=EDGE_CURVE ( 'NONE', #79129, #36317, #122557, .T. ) ;
#68772=VECTOR ( 'NONE', #49449, 999.9999999999998863 ) ;
#68773=PLANE ( 'NONE',  #34635 ) ;
#68774=CARTESIAN_POINT ( 'NONE',  ( 21.18398860626899349, 28.73617430169802134, 5.000000000000000000 ) ) ;
#68775=VERTEX_POINT ( 'NONE', #13780 ) ;
#68776=DIRECTION ( 'NONE',  ( 0.3543493200069162685, -0.000000000000000000, -0.9351131265310288487 ) ) ;
#68777=VECTOR ( 'NONE', #89088, 1000.000000000000000 ) ;
#68778=VERTEX_POINT ( 'NONE', #2928 ) ;
#68779=CARTESIAN_POINT ( 'NONE',  ( 0.000000000000000000, 0.000000000000000000, 5.000000000000000000 ) ) ;
#68780=ORIENTED_EDGE ( 'NONE', *, *, #113374, .T. ) ;
#68782=EDGE_LOOP ( 'NONE', ( #24179, #67231, #6865, #99923 ) ) ;
#68784=ORIENTED_EDGE ( 'NONE', *, *, #38911, .T. ) ;
#68785=ORIENTED_EDGE ( 'NONE', *, *, #46669, .F. ) ;
#68786=ORIENTED_EDGE ( 'NONE', *, *, #86774, .F. ) ;
#68787=EDGE_CURVE ( 'NONE', #122293, #90522, #81239, .T. ) ;
#68789=DIRECTION ( 'NONE',  ( -0.7071067811865486830, -0.7071067811865464625, 0.000000000000000000 ) ) ;
#68790=CARTESIAN_POINT ( 'NONE',  ( -2.999999999999964473, 11.58746187583912324, 4.000000000000000000 ) ) ;
#68792=CARTESIAN_POINT ( 'NONE',  ( 11.20710678118646619, -8.240707523384200428, 5.000000000000000000 ) ) ;
#68796=EDGE_CURVE ( 'NONE', #108299, #110346, #124718, .T. ) ;
#68797=DIRECTION ( 'NONE',  ( 0.6830127018922180770, -0.6830127018922204085, -0.2588190451025213501 ) ) ;
#68799=CARTESIAN_POINT ( 'NONE',  ( -17.48334561358942807, 22.22500000000000142, 4.500000000000000888 ) ) ;
#68801=VERTEX_POINT ( 'NONE', #123320 ) ;
#68803=CARTESIAN_POINT ( 'NONE',  ( -15.29974487139158867, -27.71228299555216879, 4.000000000000000000 ) ) ;
#68804=VECTOR ( 'NONE', #138833, 1000.000000000000000 ) ;
#68805=EDGE_CURVE ( 'NONE', #109084, #3210, #58079, .T. ) ;
#68806=VERTEX_POINT ( 'NONE', #79840 ) ;
#68808=CARTESIAN_POINT ( 'NONE',  ( -83.99451991528748351, 28.92564299267996830, 4.000000000000000000 ) ) ;
#68809=VERTEX_POINT ( 'NONE', #24683 ) ;
#68811=CARTESIAN_POINT ( 'NONE',  ( 32.99999999999977263, -15.41253812416059787, 4.000000000000000000 ) ) ;
#68812=AXIS2_PLACEMENT_3D ( 'NONE', #133633, #89403, #115210 ) ;
#68813=EDGE_CURVE ( 'NONE', #86982, #141725, #68942, .T. ) ;
#68814=PLANE ( 'NONE',  #27782 ) ;
#68815=CARTESIAN_POINT ( 'NONE',  ( 4.499999999999972466, -2.568876922607793212, 4.000000000000000000 ) ) ;
#68816=ORIENTED_EDGE ( 'NONE', *, *, #130097, .F. ) ;
#68818=ORIENTED_EDGE ( 'NONE', *, *, #87884, .F. ) ;
#68819=VECTOR ( 'NONE', #112758, 999.9999999999998863 ) ;
#68820=VECTOR ( 'NONE', #52499, 1000.000000000000000 ) ;
#68821=CARTESIAN_POINT ( 'NONE',  ( -36.18398860626899705, 28.73617430169812437, 5.000000000000000000 ) ) ;
#68823=AXIS2_PLACEMENT_3D ( 'NONE', #117520, #18194, #108062 ) ;
#68825=ORIENTED_EDGE ( 'NONE', *, *, #21075, .F. ) ;
#68827=PLANE ( 'NONE',  #53555 ) ;
#68829=VECTOR ( 'NONE', #111479, 999.9999999999998863 ) ;
#68830=ORIENTED_EDGE ( 'NONE', *, *, #15119, .F. ) ;
#68831=ORIENTED_EDGE ( 'NONE', *, *, #36153, .T. ) ;
#68832=CARTESIAN_POINT ( 'NONE',  ( -42.48921356237308800, -27.52281430457085065, 5.000000000000000000 ) ) ;
#68833=CARTESIAN_POINT ( 'NONE',  ( -0.1839886062690032631, 28.73617430169787568, 5.000000000000000000 ) ) ;
#68834=AXIS2_PLACEMENT_3D ( 'NONE', #71222, #16055, #69077 ) ;
#68835=CARTESIAN_POINT ( 'NONE',  ( -34.49999999999975842, -12.66682484999669178, -0.6294897503864747002 ) ) ;
#68836=CARTESIAN_POINT ( 'NONE',  ( 18.18398860626898994, 28.73617430169800002, 5.000000000000000000 ) ) ;
#68837=ORIENTED_EDGE ( 'NONE', *, *, #6210, .F. ) ;
#68838=CARTESIAN_POINT ( 'NONE',  ( -9.328169399223462221, -6.740707523384216415, 4.000000000000000000 ) ) ;
#68839=EDGE_CURVE ( 'NONE', #40167, #31872, #113115, .T. ) ;
#68840=CARTESIAN_POINT ( 'NONE',  ( 33.18398860626899705, 28.73617430169810305, 5.000000000000000000 ) ) ;
#68841=DIRECTION ( 'NONE',  ( -0.000000000000000000, -0.3543493200069152693, 0.9351131265310292928 ) ) ;
#68842=VERTEX_POINT ( 'NONE', #102278 ) ;
#68843=CARTESIAN_POINT ( 'NONE',  ( 3.328169399223507519, 8.259292476615634371, 4.000000000000000000 ) ) ;
#68844=EDGE_LOOP ( 'NONE', ( #12629, #135500, #47244, #54331 ) ) ;
#68845=ADVANCED_FACE ( 'NONE', ( #36293 ), #80522, .T. ) ;
#68846=LINE ( 'NONE', #126069, #88020 ) ;
#68847=VERTEX_POINT ( 'NONE', #47906 ) ;
#68848=VERTEX_POINT ( 'NONE', #73213 ) ;
#68849=EDGE_CURVE ( 'NONE', #23467, #14718, #126159, .T. ) ;
#68850=DIRECTION ( 'NONE',  ( -0.7071067811865487940, 0.7071067811865463515, 0.000000000000000000 ) ) ;
#68851=CARTESIAN_POINT ( 'NONE',  ( 34.45011844616453089, -20.99769585840584085, 5.000000000000000888 ) ) ;
#68852=VECTOR ( 'NONE', #109238, 1000.000000000000000 ) ;
#68853=ORIENTED_EDGE ( 'NONE', *, *, #100926, .T. ) ;
#68854=DIRECTION ( 'NONE',  ( 0.6830127018922181881, 0.6830127018922202975, -0.2588190451025214056 ) ) ;
#68855=ORIENTED_EDGE ( 'NONE', *, *, #107350, .T. ) ;
#68856=( BOUNDED_CURVE ( )  B_SPLINE_CURVE ( 3, ( #142552, #76595, #130251, #22158 ),
 .UNSPECIFIED., .F., .T. ) 
 B_SPLINE_CURVE_WITH_KNOTS ( ( 4, 4 ),
 ( 5.584306267627116682, 5.657315652343092971 ),
 .UNSPECIFIED. ) 
 CURVE ( )  GEOMETRIC_REPRESENTATION_ITEM ( )  RATIONAL_B_SPLINE_CURVE ( ( 1.000000000000000000, 0.9995558518042845231, 0.9995558518042845231, 1.000000000000000000 ) ) 
 REPRESENTATION_ITEM ( '' )  );
#68857=LINE ( 'NONE', #89162, #5829 ) ;
#68858=PLANE ( 'NONE',  #83329 ) ;
#68859=VECTOR ( 'NONE', #95542, 1000.000000000000000 ) ;
#68860=DIRECTION ( 'NONE',  ( 0.7071067811865487940, -0.7071067811865463515, 0.000000000000000000 ) ) ;
#68861=CARTESIAN_POINT ( 'NONE',  ( -16.17183060077636370, -20.24070752338408141, 4.000000000000000000 ) ) ;
#68862=CARTESIAN_POINT ( 'NONE',  ( -17.81601139373099940, 28.73617430169775133, 5.000000000000000000 ) ) ;
#68863=CARTESIAN_POINT ( 'NONE',  ( -34.92500000000001137, 0.7592924766157104211, 4.255531930566247567 ) ) ;
#68864=DIRECTION ( 'NONE',  ( 0.7071067811865487940, 0.7071067811865463515, 0.000000000000000000 ) ) ;
#68865=DIRECTION ( 'NONE',  ( -0.000000000000000000, 0.000000000000000000, 1.000000000000000000 ) ) ;
#68869=DIRECTION ( 'NONE',  ( 0.7071067811865486830, -0.7071067811865464625, -0.000000000000000000 ) ) ;
#68870=PLANE ( 'NONE',  #2652 ) ;
#68871=DIRECTION ( 'NONE',  ( 1.000000000000000000, 0.000000000000000000, 0.000000000000000000 ) ) ;
#68873=EDGE_CURVE ( 'NONE', #129051, #124700, #39882, .T. ) ;
#68874=VERTEX_POINT ( 'NONE', #115222 ) ;
#68876=ORIENTED_EDGE ( 'NONE', *, *, #118641, .F. ) ;
#68877=ORIENTED_EDGE ( 'NONE', *, *, #56019, .F. ) ;
#68878=ORIENTED_EDGE ( 'NONE', *, *, #82185, .T. ) ;
#68879=VECTOR ( 'NONE', #2687, 1000.000000000000000 ) ;
#68880=LINE ( 'NONE', #56602, #36465 ) ;
#68881=CARTESIAN_POINT ( 'NONE',  ( 69.48921356237309510, -27.52281430457103895, 5.000000000000000000 ) ) ;
#68882=CARTESIAN_POINT ( 'NONE',  ( 66.29974487139159578, -27.71228299555252406, 4.000000000000000000 ) ) ;
#68883=VERTEX_POINT ( 'NONE', #104375 ) ;
#68884=DIRECTION ( 'NONE',  ( 0.7071067811865486830, -0.7071067811865464625, -0.000000000000000000 ) ) ;
#68886=PLANE ( 'NONE',  #118103 ) ;
#68887=LINE ( 'NONE', #113060, #139239 ) ;
#68890=DIRECTION ( 'NONE',  ( 0.7071067811865487940, 0.7071067811865463515, 0.000000000000000000 ) ) ;
#68891=CARTESIAN_POINT ( 'NONE',  ( 34.45011844616451668, 22.22500000000000142, 4.231322045535989673 ) ) ;
#68892=CARTESIAN_POINT ( 'NONE',  ( 24.96654721599509941, 3.964575861396866685, 4.000000000000000000 ) ) ;
#68893=DIRECTION ( 'NONE',  ( 0.3543493200069162685, -0.000000000000000000, -0.9351131265310288487 ) ) ;
#68895=DIRECTION ( 'NONE',  ( 1.000000000000000000, 0.000000000000000000, 0.000000000000000000 ) ) ;
#68898=EDGE_CURVE ( 'NONE', #123192, #46180, #117377, .T. ) ;
#68900=AXIS2_PLACEMENT_3D ( 'NONE', #33638, #133648, #34325 ) ;
#68902=ORIENTED_EDGE ( 'NONE', *, *, #19138, .T. ) ;
#68903=EDGE_CURVE ( 'NONE', #83531, #131076, #26826, .T. ) ;
#68904=CARTESIAN_POINT ( 'NONE',  ( -32.99999999999975842, 14.96639925780210767, 5.000000000000000000 ) ) ;
#68906=EDGE_CURVE ( 'NONE', #126702, #44187, #128303, .T. ) ;
#68908=DIRECTION ( 'NONE',  ( -0.6830127018922180770, -0.6830127018922204085, -0.2588190451025213501 ) ) ;
#68909=CARTESIAN_POINT ( 'NONE',  ( 30.18398860626900060, 28.73617430169808173, 5.000000000000000000 ) ) ;
#68910=VECTOR ( 'NONE', #140861, 1000.000000000000000 ) ;
#68912=EDGE_LOOP ( 'NONE', ( #69013, #82707, #16194, #46473 ) ) ;
#68913=EDGE_LOOP ( 'NONE', ( #141334, #142839, #127361, #25326 ) ) ;
#68914=DIRECTION ( 'NONE',  ( 0.7071067811865487940, 0.7071067811865463515, 0.000000000000000000 ) ) ;
#68915=CARTESIAN_POINT ( 'NONE',  ( 27.48921356237309155, -27.52281430457074762, 5.000000000000000000 ) ) ;
#68917=EDGE_LOOP ( 'NONE', ( #67352, #106791, #45737, #73268 ) ) ;
#68918=ORIENTED_EDGE ( 'NONE', *, *, #138746, .F. ) ;
#68919=AXIS2_PLACEMENT_3D ( 'NONE', #14159, #70026, #39519 ) ;
#68920=EDGE_CURVE ( 'NONE', #56677, #76836, #84782, .T. ) ;
#68921=EDGE_LOOP ( 'NONE', ( #89340, #59188, #8634, #28109 ) ) ;
#68923=ADVANCED_FACE ( 'NONE', ( #7180 ), #50029, .F. ) ;
#68925=VECTOR ( 'NONE', #17387, 1000.000000000000227 ) ;
#68927=EDGE_CURVE ( 'NONE', #93801, #43398, #118082, .T. ) ;
#68930=ORIENTED_EDGE ( 'NONE', *, *, #36098, .F. ) ;
#68931=VERTEX_POINT ( 'NONE', #18792 ) ;
#68932=CARTESIAN_POINT ( 'NONE',  ( -29.20710678118633297, 0.7592924766157086447, 5.000000000000000000 ) ) ;
#68933=VERTEX_POINT ( 'NONE', #37730 ) ;
#68934=VERTEX_POINT ( 'NONE', #115956 ) ;
#68935=AXIS2_PLACEMENT_3D ( 'NONE', #130599, #25185, #68048 ) ;
#68936=ADVANCED_FACE ( 'NONE', ( #16660 ), #60943, .F. ) ;
#68937=VERTEX_POINT ( 'NONE', #138458 ) ;
#68938=FACE_OUTER_BOUND ( 'NONE', #27705, .T. ) ;
#68940=LINE ( 'NONE', #89239, #30281 ) ;
#68941=ORIENTED_EDGE ( 'NONE', *, *, #42696, .F. ) ;
#68942=LINE ( 'NONE', #91400, #131701 ) ;
#68943=EDGE_CURVE ( 'NONE', #68281, #87685, #39147, .T. ) ;
#68944=DIRECTION ( 'NONE',  ( 0.7071067811865486830, -0.7071067811865464625, -0.000000000000000000 ) ) ;
#68946=FACE_BOUND ( 'NONE', #48462, .T. ) ;
#68947=ORIENTED_EDGE ( 'NONE', *, *, #138589, .F. ) ;
#68949=LINE ( 'NONE', #2938, #131805 ) ;
#68950=DIRECTION ( 'NONE',  ( -0.3543493200069162685, -0.000000000000000000, -0.9351131265310288487 ) ) ;
#68951=EDGE_LOOP ( 'NONE', ( #88743, #39471, #120699 ) ) ;
#68952=EDGE_CURVE ( 'NONE', #53759, #112632, #4290, .T. ) ;
#68953=CARTESIAN_POINT ( 'NONE',  ( 36.18398860626899705, 28.73617430169812437, 5.000000000000000000 ) ) ;
#68954=ORIENTED_EDGE ( 'NONE', *, *, #21440, .F. ) ;
#68955=VECTOR ( 'NONE', #112643, 1000.000000000000000 ) ;
#68956=EDGE_CURVE ( 'NONE', #12982, #136524, #62340, .T. ) ;
#68957=VERTEX_POINT ( 'NONE', #17377 ) ;
#68958=EDGE_LOOP ( 'NONE', ( #102530, #76058, #18910, #41805 ) ) ;
#68962=ORIENTED_EDGE ( 'NONE', *, *, #66290, .T. ) ;
#68963=FACE_OUTER_BOUND ( 'NONE', #37213, .T. ) ;
#68964=CARTESIAN_POINT ( 'NONE',  ( 23.24139925780185223, 21.72500000000000853, 5.000000000000000000 ) ) ;
#68965=ORIENTED_EDGE ( 'NONE', *, *, #96369, .T. ) ;
#68967=LINE ( 'NONE', #104407, #141768 ) ;
#68969=CARTESIAN_POINT ( 'NONE',  ( 7.371765549556104524, -8.240707523384203981, 11.38925528200750925 ) ) ;
#68972=ORIENTED_EDGE ( 'NONE', *, *, #98631, .F. ) ;
#68973=ORIENTED_EDGE ( 'NONE', *, *, #121577, .T. ) ;
#68974=EDGE_LOOP ( 'NONE', ( #110224, #38484, #79919, #43598 ) ) ;
#68975=VERTEX_POINT ( 'NONE', #108635 ) ;
#68976=ORIENTED_EDGE ( 'NONE', *, *, #124388, .T. ) ;
#68977=ORIENTED_EDGE ( 'NONE', *, *, #26518, .F. ) ;
#68978=CARTESIAN_POINT ( 'NONE',  ( 69.48921356237309510, -27.52281430457103895, 5.000000000000000000 ) ) ;
#68979=DIRECTION ( 'NONE',  ( -0.000000000000000000, -0.3543493200069152693, 0.9351131265310292928 ) ) ;
#68981=DIRECTION ( 'NONE',  ( -0.000000000000000000, 0.000000000000000000, 1.000000000000000000 ) ) ;
#68982=ORIENTED_EDGE ( 'NONE', *, *, #65669, .F. ) ;
#68988=PLANE ( 'NONE',  #97624 ) ;
#68989=DIRECTION ( 'NONE',  ( 0.7071067811865486830, -0.7071067811865464625, -0.000000000000000000 ) ) ;
#68990=EDGE_CURVE ( 'NONE', #137546, #89076, #98509, .T. ) ;
#68991=ORIENTED_EDGE ( 'NONE', *, *, #76840, .F. ) ;
#68992=CARTESIAN_POINT ( 'NONE',  ( 17.99999999999987210, 10.93112307739206912, 4.000000000000000000 ) ) ;
#68993=LINE ( 'NONE', #2248, #49251 ) ;
#68994=VERTEX_POINT ( 'NONE', #9309 ) ;
#68995=DIRECTION ( 'NONE',  ( 0.7071067811865486830, -0.7071067811865464625, -0.000000000000000000 ) ) ;
#68996=CARTESIAN_POINT ( 'NONE',  ( 22.49999999999984013, 10.08746187583914633, 4.000000000000000000 ) ) ;
#68997=CARTESIAN_POINT ( 'NONE',  ( 15.48921356237309510, -27.52281430457066236, 5.000000000000000000 ) ) ;
#68999=DIRECTION ( 'NONE',  ( -0.000000000000000000, -0.3543493200069153248, 0.9351131265310292928 ) ) ;
#69000=DIRECTION ( 'NONE',  ( 0.6830127018922180770, -0.6830127018922204085, -0.2588190451025213501 ) ) ;
#69002=DIRECTION ( 'NONE',  ( 0.000000000000000000, -1.000000000000000000, 0.000000000000000000 ) ) ;
#69003=VECTOR ( 'NONE', #3052, 1000.000000000000000 ) ;
#69004=LINE ( 'NONE', #113182, #58158 ) ;
#69005=DIRECTION ( 'NONE',  ( 0.7071067811865487940, -0.7071067811865463515, 0.000000000000000000 ) ) ;
#69006=ORIENTED_EDGE ( 'NONE', *, *, #42424, .T. ) ;
#69007=VECTOR ( 'NONE', #71468, 1000.000000000000000 ) ;
#69008=LINE ( 'NONE', #15990, #111803 ) ;
#69009=ORIENTED_EDGE ( 'NONE', *, *, #137421, .F. ) ;
#69010=VECTOR ( 'NONE', #24871, 1000.000000000000000 ) ;
#69011=EDGE_CURVE ( 'NONE', #135494, #141475, #99194, .T. ) ;
#69012=PLANE ( 'NONE',  #101881 ) ;
#69013=ORIENTED_EDGE ( 'NONE', *, *, #85182, .T. ) ;
#69015=EDGE_CURVE ( 'NONE', #106679, #64810, #42006, .T. ) ;
#69016=ORIENTED_EDGE ( 'NONE', *, *, #22758, .F. ) ;
#69017=CARTESIAN_POINT ( 'NONE',  ( 8.671830600776416986, -3.740707523384241728, 4.000000000000000000 ) ) ;
#69019=AXIS2_PLACEMENT_3D ( 'NONE', #82169, #126345, #90146 ) ;
#69020=ORIENTED_EDGE ( 'NONE', *, *, #56068, .F. ) ;
#69021=VECTOR ( 'NONE', #56505, 1000.000000000000000 ) ;
#69022=ORIENTED_EDGE ( 'NONE', *, *, #90339, .T. ) ;
#69024=LINE ( 'NONE', #113203, #51235 ) ;
#69025=CARTESIAN_POINT ( 'NONE',  ( 33.18398860626899705, 28.73617430169810305, 5.000000000000000000 ) ) ;
#69026=LINE ( 'NONE', #113205, #95668 ) ;
#69027=CARTESIAN_POINT ( 'NONE',  ( 2.671830600776463172, 8.259292476615646805, 4.000000000000000000 ) ) ;
#69030=LINE ( 'NONE', #27632, #43068 ) ;
#69031=ORIENTED_EDGE ( 'NONE', *, *, #22116, .F. ) ;
#69032=EDGE_CURVE ( 'NONE', #25524, #42897, #63764, .T. ) ;
#69033=VERTEX_POINT ( 'NONE', #109386 ) ;
#69034=ORIENTED_EDGE ( 'NONE', *, *, #121692, .T. ) ;
#69036=VERTEX_POINT ( 'NONE', #140574 ) ;
#69037=ORIENTED_EDGE ( 'NONE', *, *, #25832, .T. ) ;
#69038=ORIENTED_EDGE ( 'NONE', *, *, #137910, .F. ) ;
#69040=CARTESIAN_POINT ( 'NONE',  ( -48.18398860626899705, 28.73617430169820608, 5.000000000000000000 ) ) ;
#69041=EDGE_CURVE ( 'NONE', #79941, #102767, #131866, .T. ) ;
#69042=ORIENTED_EDGE ( 'NONE', *, *, #37918, .F. ) ;
#69044=CARTESIAN_POINT ( 'NONE',  ( 34.49999999999976552, -9.462702396500981550, -9.474982329943593129 ) ) ;
#69046=PLANE ( 'NONE',  #32414 ) ;
#69047=FACE_OUTER_BOUND ( 'NONE', #36442, .T. ) ;
#69049=ORIENTED_EDGE ( 'NONE', *, *, #47036, .F. ) ;
#69050=CARTESIAN_POINT ( 'NONE',  ( 23.55512991947088963, -0.7407075233842735917, 4.307968247157003994 ) ) ;
#69051=CARTESIAN_POINT ( 'NONE',  ( -12.18398860626900060, 28.73617430169795739, 5.000000000000000000 ) ) ;
#69053=CARTESIAN_POINT ( 'NONE',  ( 2.671830600776449405, -6.740707523384212863, 4.000000000000000000 ) ) ;
#69056=CARTESIAN_POINT ( 'NONE',  ( -42.29974487139158157, -27.71228299555235708, 4.000000000000000000 ) ) ;
#69057=LINE ( 'NONE', #134308, #138425 ) ;
#69060=DIRECTION ( 'NONE',  ( 0.6830127018922181881, 0.6830127018922202975, -0.2588190451025214056 ) ) ;
#69061=ORIENTED_EDGE ( 'NONE', *, *, #137451, .T. ) ;
#69064=ORIENTED_EDGE ( 'NONE', *, *, #129795, .F. ) ;
#69065=CARTESIAN_POINT ( 'NONE',  ( -24.48921356237309510, -27.52281430457072631, 5.000000000000000000 ) ) ;
#69066=EDGE_CURVE ( 'NONE', #73197, #95699, #32554, .T. ) ;
#69068=AXIS2_PLACEMENT_3D ( 'NONE', #60222, #5064, #83392 ) ;
#69069=LINE ( 'NONE', #115364, #82786 ) ;
#69071=DIRECTION ( 'NONE',  ( 0.7071067811865487940, 0.7071067811865463515, -0.000000000000000000 ) ) ;
#69072=AXIS2_PLACEMENT_3D ( 'NONE', #3874, #124274, #38004 ) ;
#69073=EDGE_CURVE ( 'NONE', #44746, #122630, #10756, .T. ) ;
#69074=ADVANCED_FACE ( 'NONE', ( #88371 ), #52150, .F. ) ;
#69076=EDGE_LOOP ( 'NONE', ( #60506, #67723, #94547, #103811 ) ) ;
#69077=DIRECTION ( 'NONE',  ( 0.7071067811865487940, 0.7071067811865463515, 0.000000000000000000 ) ) ;
#69078=VERTEX_POINT ( 'NONE', #130446 ) ;
#69079=LINE ( 'NONE', #113256, #12580 ) ;
#69080=EDGE_CURVE ( 'NONE', #41509, #142587, #142045, .T. ) ;
#69081=DIRECTION ( 'NONE',  ( -0.7071067811865486830, 0.7071067811865464625, 0.000000000000000000 ) ) ;
#69083=CARTESIAN_POINT ( 'NONE',  ( 44.99451991528749772, 28.92564299267969474, 4.000000000000000000 ) ) ;
#69084=ORIENTED_EDGE ( 'NONE', *, *, #92385, .F. ) ;
#69085=ADVANCED_FACE ( 'NONE', ( #86934 ), #74640, .T. ) ;
#69086=LINE ( 'NONE', #60168, #7176 ) ;
#69087=VERTEX_POINT ( 'NONE', #76052 ) ;
#69089=EDGE_CURVE ( 'NONE', #65792, #32200, #120222, .T. ) ;
#69090=DIRECTION ( 'NONE',  ( -0.7071067811865487940, 0.7071067811865463515, -0.000000000000000000 ) ) ;
#69091=LINE ( 'NONE', #113269, #105605 ) ;
#69092=DIRECTION ( 'NONE',  ( 0.3543493200069162685, -0.000000000000000000, -0.9351131265310288487 ) ) ;
#69093=AXIS2_PLACEMENT_3D ( 'NONE', #58298, #89434, #102480 ) ;
#69097=CARTESIAN_POINT ( 'NONE',  ( -25.00934544866806064, 2.809161053235901484, 4.346514962826536710 ) ) ;
#69098=CARTESIAN_POINT ( 'NONE',  ( 36.29974487139159578, -27.71228299555231445, 4.000000000000000000 ) ) ;
#69099=VERTEX_POINT ( 'NONE', #12205 ) ;
#69100=EDGE_LOOP ( 'NONE', ( #26062, #140083, #14702, #3487 ) ) ;
#69102=ADVANCED_FACE ( 'NONE', ( #11468 ), #3454, .F. ) ;
#69103=ORIENTED_EDGE ( 'NONE', *, *, #12405, .F. ) ;
#69104=DIRECTION ( 'NONE',  ( -0.6830127018922180770, -0.6830127018922204085, -0.2588190451025213501 ) ) ;
#69105=ORIENTED_EDGE ( 'NONE', *, *, #48801, .F. ) ;
#69106=CARTESIAN_POINT ( 'NONE',  ( -13.25154412867567189, -11.24070752338417201, 10.39518518046012119 ) ) ;
#69107=CARTESIAN_POINT ( 'NONE',  ( -12.32816939922343913, -15.74070752338412404, 4.000000000000000000 ) ) ;
#69108=PLANE ( 'NONE',  #67363 ) ;
#69109=VECTOR ( 'NONE', #20029, 1000.000000000000000 ) ;
#69110=FACE_BOUND ( 'NONE', #36494, .T. ) ;
#69111=LINE ( 'NONE', #113293, #17824 ) ;
#69113=CARTESIAN_POINT ( 'NONE',  ( 3.005480084712505828, 28.92564299267936079, 4.000000000000000000 ) ) ;
#69114=CARTESIAN_POINT ( 'NONE',  ( -16.49999999999988276, 21.05218569542895679, 5.000000000000000000 ) ) ;
#69115=DIRECTION ( 'NONE',  ( -0.7071067811865486830, -0.7071067811865464625, -0.000000000000000000 ) ) ;
#69117=EDGE_LOOP ( 'NONE', ( #58724, #51371, #70824, #125306 ) ) ;
#69118=VECTOR ( 'NONE', #34908, 1000.000000000000000 ) ;
#69119=EDGE_LOOP ( 'NONE', ( #18370, #78453, #93560, #82274 ) ) ;
#69120=VECTOR ( 'NONE', #125715, 1000.000000000000000 ) ;
#69122=ORIENTED_EDGE ( 'NONE', *, *, #88510, .F. ) ;
#69123=EDGE_CURVE ( 'NONE', #47403, #138017, #44904, .T. ) ;
#69125=ORIENTED_EDGE ( 'NONE', *, *, #100962, .T. ) ;
#69127=ORIENTED_EDGE ( 'NONE', *, *, #30596, .T. ) ;
#69128=DIRECTION ( 'NONE',  ( 0.7071067811865487940, -0.7071067811865463515, 0.000000000000000000 ) ) ;
#69129=ORIENTED_EDGE ( 'NONE', *, *, #5808, .F. ) ;
#69130=PLANE ( 'NONE',  #53728 ) ;
#69131=VECTOR ( 'NONE', #32824, 1000.000000000000000 ) ;
#69133=VECTOR ( 'NONE', #39803, 1000.000000000000000 ) ;
#69134=CARTESIAN_POINT ( 'NONE',  ( 9.299744871391588674, -27.71228299555212971, 4.000000000000000000 ) ) ;
#69136=DIRECTION ( 'NONE',  ( 0.7071067811865487940, 0.7071067811865463515, -0.000000000000000000 ) ) ;
#69137=FACE_OUTER_BOUND ( 'NONE', #67942, .T. ) ;
#69138=DIRECTION ( 'NONE',  ( 0.7071067811865486830, 0.7071067811865464625, 0.000000000000000000 ) ) ;
#69139=PLANE ( 'NONE',  #124961 ) ;
#69140=ORIENTED_EDGE ( 'NONE', *, *, #33107, .F. ) ;
#69141=ORIENTED_EDGE ( 'NONE', *, *, #68016, .T. ) ;
#69142=LINE ( 'NONE', #66992, #107564 ) ;
#69143=DIRECTION ( 'NONE',  ( -0.000000000000000000, -0.000000000000000000, 1.000000000000000000 ) ) ;
#69145=VECTOR ( 'NONE', #80264, 1000.000000000000000 ) ;
#69146=ORIENTED_EDGE ( 'NONE', *, *, #69759, .T. ) ;
#69147=VECTOR ( 'NONE', #26855, 1000.000000000000000 ) ;
#69148=ORIENTED_EDGE ( 'NONE', *, *, #54701, .T. ) ;
#69149=LINE ( 'NONE', #88764, #36883 ) ;
#69150=ORIENTED_EDGE ( 'NONE', *, *, #8265, .T. ) ;
#69152=CARTESIAN_POINT ( 'NONE',  ( -57.48921356237308800, -27.52281430457095368, 5.000000000000000000 ) ) ;
#69153=CARTESIAN_POINT ( 'NONE',  ( 5.999999999999965361, -0.03360074219773551141, 5.000000000000000000 ) ) ;
#69157=CARTESIAN_POINT ( 'NONE',  ( 34.92499999999998295, -22.22500000000000142, 4.500000000000000888 ) ) ;
#69158=CARTESIAN_POINT ( 'NONE',  ( -17.02886364525924989, -2.441401769420105339, 4.000000000000000000 ) ) ;
#69159=DIRECTION ( 'NONE',  ( -0.7071067811865486830, -0.7071067811865464625, 0.000000000000000000 ) ) ;
#69162=ORIENTED_EDGE ( 'NONE', *, *, #66807, .T. ) ;
#69163=LINE ( 'NONE', #133008, #7931 ) ;
#69166=FACE_OUTER_BOUND ( 'NONE', #100189, .T. ) ;
#69167=VERTEX_POINT ( 'NONE', #608 ) ;
#69168=DIRECTION ( 'NONE',  ( -0.7071067811865487940, 0.7071067811865463515, -0.000000000000000000 ) ) ;
#69171=DIRECTION ( 'NONE',  ( 0.7071067811865486830, -0.7071067811865464625, -0.000000000000000000 ) ) ;
#69172=DIRECTION ( 'NONE',  ( -0.6830127018922181881, 0.6830127018922202975, -0.2588190451025214056 ) ) ;
#69173=ORIENTED_EDGE ( 'NONE', *, *, #77564, .F. ) ;
#69174=CARTESIAN_POINT ( 'NONE',  ( -30.70710678118633652, 11.25929247661560773, 5.000000000000000000 ) ) ;
#69175=LINE ( 'NONE', #113358, #56321 ) ;
#69177=EDGE_CURVE ( 'NONE', #80880, #60780, #122386, .T. ) ;
#69179=LINE ( 'NONE', #113362, #90030 ) ;
#69180=EDGE_CURVE ( 'NONE', #67296, #86133, #136131, .T. ) ;
#69181=VERTEX_POINT ( 'NONE', #81063 ) ;
#69182=ORIENTED_EDGE ( 'NONE', *, *, #53829, .F. ) ;
#69184=ADVANCED_FACE ( 'NONE', ( #33983 ), #23814, .F. ) ;
#69185=EDGE_CURVE ( 'NONE', #139146, #127658, #68080, .T. ) ;
#69186=CARTESIAN_POINT ( 'NONE',  ( 9.758600742197899081, 21.72500000000000853, 5.000000000000000000 ) ) ;
#69187=DIRECTION ( 'NONE',  ( -0.7071067811865486830, -0.7071067811865464625, 0.000000000000000000 ) ) ;
#69188=CARTESIAN_POINT ( 'NONE',  ( 8.510786437626906675, -27.52281430457049183, 5.000000000000000000 ) ) ;
#69189=CARTESIAN_POINT ( 'NONE',  ( 30.29974487139158867, -27.71228299555227537, 4.000000000000000000 ) ) ;
#69190=ORIENTED_EDGE ( 'NONE', *, *, #81329, .T. ) ;
#69191=EDGE_CURVE ( 'NONE', #87366, #135494, #110783, .T. ) ;
#69192=CARTESIAN_POINT ( 'NONE',  ( 41.99451991528749062, 28.92564299267967343, 4.000000000000000000 ) ) ;
#69194=DIRECTION ( 'NONE',  ( -0.000000000000000000, -0.3543493200069152693, 0.9351131265310292928 ) ) ;
#69195=CARTESIAN_POINT ( 'NONE',  ( -12.79289321881336328, -11.24070752338416845, 5.000000000000000000 ) ) ;
#69197=LINE ( 'NONE', #112681, #18583 ) ;
#69198=EDGE_CURVE ( 'NONE', #123136, #39115, #91910, .T. ) ;
#69201=ORIENTED_EDGE ( 'NONE', *, *, #102914, .F. ) ;
#69203=ORIENTED_EDGE ( 'NONE', *, *, #3439, .F. ) ;
#69206=EDGE_CURVE ( 'NONE', #42509, #64814, #112259, .T. ) ;
#69207=VECTOR ( 'NONE', #52575, 999.9999999999998863 ) ;
#69208=VECTOR ( 'NONE', #135606, 1000.000000000000000 ) ;
#69209=CARTESIAN_POINT ( 'NONE',  ( 28.49999999999980460, 10.94296225409028800, -9.576120664313192421 ) ) ;
#69210=DIRECTION ( 'NONE',  ( -0.3543493200069163240, 4.681814790819596721E-17, -0.9351131265310288487 ) ) ;
#69211=VECTOR ( 'NONE', #23817, 999.9999999999998863 ) ;
#69212=DIRECTION ( 'NONE',  ( 0.6830127018922181881, 0.6830127018922202975, -0.2588190451025214056 ) ) ;
#69213=CARTESIAN_POINT ( 'NONE',  ( 13.17183060077638324, -8.240707523384196875, 4.000000000000000000 ) ) ;
#69215=ORIENTED_EDGE ( 'NONE', *, *, #89484, .T. ) ;
#69216=ORIENTED_EDGE ( 'NONE', *, *, #56983, .F. ) ;
#69218=CARTESIAN_POINT ( 'NONE',  ( -24.18398860626899705, 28.73617430169804265, 5.000000000000000000 ) ) ;
#69220=EDGE_CURVE ( 'NONE', #46380, #77993, #57187, .T. ) ;
#69221=VECTOR ( 'NONE', #3867, 1000.000000000000114 ) ;
#69222=DIRECTION ( 'NONE',  ( 0.6830127018922181881, 0.6830127018922202975, -0.2588190451025214056 ) ) ;
#69223=DIRECTION ( 'NONE',  ( 0.7071067811865487940, 0.7071067811865463515, -0.000000000000000000 ) ) ;
#69225=DIRECTION ( 'NONE',  ( -0.000000000000000000, 0.000000000000000000, 1.000000000000000000 ) ) ;
#69226=DIRECTION ( 'NONE',  ( -0.3543493200069162685, -0.000000000000000000, -0.9351131265310288487 ) ) ;
#69227=VERTEX_POINT ( 'NONE', #46318 ) ;
#69229=CARTESIAN_POINT ( 'NONE',  ( -0.1839886062690032631, 28.73617430169787568, 5.000000000000000000 ) ) ;
#69230=DIRECTION ( 'NONE',  ( -0.6830127018922181881, 0.6830127018922202975, -0.2588190451025214056 ) ) ;
#69231=CARTESIAN_POINT ( 'NONE',  ( 21.85005128541011388, -8.240707523384182664, 17.25253755692243729 ) ) ;
#69232=ADVANCED_FACE ( 'NONE', ( #113661 ), #90500, .T. ) ;
#69234=ORIENTED_EDGE ( 'NONE', *, *, #88055, .T. ) ;
#69235=FACE_OUTER_BOUND ( 'NONE', #22248, .T. ) ;
#69237=VECTOR ( 'NONE', #91670, 1000.000000000000114 ) ;
#69238=PLANE ( 'NONE',  #95328 ) ;
#69240=EDGE_CURVE ( 'NONE', #127203, #37030, #14359, .T. ) ;
#69241=PLANE ( 'NONE',  #92258 ) ;
#69243=VERTEX_POINT ( 'NONE', #60767 ) ;
#69244=VECTOR ( 'NONE', #39661, 1000.000000000000000 ) ;
#69245=EDGE_CURVE ( 'NONE', #68883, #27289, #60021, .T. ) ;
#69246=DIRECTION ( 'NONE',  ( -0.7071067811865486830, -0.7071067811865464625, 0.000000000000000000 ) ) ;
#69247=DIRECTION ( 'NONE',  ( -0.7071067811865486830, -0.7071067811865464625, 0.000000000000000000 ) ) ;
#69248=LINE ( 'NONE', #24992, #57876 ) ;
#69249=CARTESIAN_POINT ( 'NONE',  ( -10.49999999999991829, -11.94781430457070748, 5.000000000000000000 ) ) ;
#69250=EDGE_LOOP ( 'NONE', ( #94060, #47783, #125610, #70886 ) ) ;
#69251=CARTESIAN_POINT ( 'NONE',  ( 42.48921356237308800, -27.52281430457085065, 5.000000000000000000 ) ) ;
#69253=CARTESIAN_POINT ( 'NONE',  ( 63.29974487139158867, -27.71228299555250274, 4.000000000000000000 ) ) ;
#69254=VECTOR ( 'NONE', #18706, 999.9999999999998863 ) ;
#69255=LINE ( 'NONE', #47537, #20637 ) ;
#69257=VERTEX_POINT ( 'NONE', #94049 ) ;
#69258=VERTEX_POINT ( 'NONE', #138285 ) ;
#69260=ORIENTED_EDGE ( 'NONE', *, *, #95829, .F. ) ;
#69261=EDGE_CURVE ( 'NONE', #94085, #80926, #137574, .T. ) ;
#69263=LINE ( 'NONE', #2529, #73511 ) ;
#69264=DIRECTION ( 'NONE',  ( -0.7071067811865486830, -0.7071067811865464625, 0.000000000000000000 ) ) ;
#69265=DIRECTION ( 'NONE',  ( -0.6830127018922180770, -0.6830127018922204085, -0.2588190451025213501 ) ) ;
#69266=CARTESIAN_POINT ( 'NONE',  ( 39.29974487139159578, -27.71228299555233576, 4.000000000000000000 ) ) ;
#69268=ORIENTED_EDGE ( 'NONE', *, *, #102783, .F. ) ;
#69269=AXIS2_PLACEMENT_3D ( 'NONE', #75598, #108892, #10308 ) ;
#69273=ORIENTED_EDGE ( 'NONE', *, *, #78062, .F. ) ;
#69274=DIRECTION ( 'NONE',  ( -0.3543493200069162685, -0.000000000000000000, -0.9351131265310288487 ) ) ;
#69276=LINE ( 'NONE', #113456, #140591 ) ;
#69277=DIRECTION ( 'NONE',  ( -0.6830127018922180770, -0.6830127018922204085, -0.2588190451025213501 ) ) ;
#69278=ORIENTED_EDGE ( 'NONE', *, *, #77324, .T. ) ;
#69279=FACE_BOUND ( 'NONE', #54133, .T. ) ;
#69280=CARTESIAN_POINT ( 'NONE',  ( -36.18398860626899705, 28.73617430169812437, 5.000000000000000000 ) ) ;
#69281=ADVANCED_FACE ( 'NONE', ( #83190 ), #126668, .F. ) ;
#69282=DIRECTION ( 'NONE',  ( -0.7071067811865486830, 0.7071067811865464625, 0.000000000000000000 ) ) ;
#69283=DIRECTION ( 'NONE',  ( -0.6830127018922180770, -0.6830127018922204085, -0.2588190451025213501 ) ) ;
#69284=DIRECTION ( 'NONE',  ( 0.6830127018922180770, -0.6830127018922204085, -0.2588190451025213501 ) ) ;
#69287=ORIENTED_EDGE ( 'NONE', *, *, #13597, .F. ) ;
#69288=ADVANCED_FACE ( 'NONE', ( #28091 ), #117210, .F. ) ;
#69289=ORIENTED_EDGE ( 'NONE', *, *, #65775, .T. ) ;
#69292=FACE_OUTER_BOUND ( 'NONE', #10671, .T. ) ;
#69294=CARTESIAN_POINT ( 'NONE',  ( 0.000000000000000000, 0.000000000000000000, 5.000000000000000000 ) ) ;
#69295=CARTESIAN_POINT ( 'NONE',  ( 0.000000000000000000, 0.000000000000000000, 5.000000000000000000 ) ) ;
#69296=CARTESIAN_POINT ( 'NONE',  ( -2.994519915287485734, 28.92564299267940342, 4.000000000000000000 ) ) ;
#69302=DIRECTION ( 'NONE',  ( 0.7071067811865487940, 0.7071067811865463515, 0.000000000000000000 ) ) ;
#69303=CARTESIAN_POINT ( 'NONE',  ( -33.51168605928411637, 6.759292476615653023, 16.35960578974477286 ) ) ;
#69304=CARTESIAN_POINT ( 'NONE',  ( 2.816011393730999401, 28.73617430169785436, 5.000000000000000000 ) ) ;
#69305=VECTOR ( 'NONE', #42946, 1000.000000000000000 ) ;
#69306=VECTOR ( 'NONE', #47232, 1000.000000000000000 ) ;
#69307=CARTESIAN_POINT ( 'NONE',  ( -32.99999999999977263, 4.931123077392136622, 4.000000000000000000 ) ) ;
#69308=AXIS2_PLACEMENT_3D ( 'NONE', #114164, #70699, #51065 ) ;
#69311=DIRECTION ( 'NONE',  ( 0.7071067811865487940, 0.7071067811865463515, 0.000000000000000000 ) ) ;
#69312=AXIS2_PLACEMENT_3D ( 'NONE', #42572, #88200, #132451 ) ;
#69313=ORIENTED_EDGE ( 'NONE', *, *, #104776, .F. ) ;
#69314=ORIENTED_EDGE ( 'NONE', *, *, #116323, .F. ) ;
#69315=EDGE_CURVE ( 'NONE', #100866, #21087, #83935, .T. ) ;
#69316=ORIENTED_EDGE ( 'NONE', *, *, #143322, .T. ) ;
#69318=ORIENTED_EDGE ( 'NONE', *, *, #740, .T. ) ;
#69319=VECTOR ( 'NONE', #91480, 1000.000000000000227 ) ;
#69322=CARTESIAN_POINT ( 'NONE',  ( 23.90156419391748699, 11.25929247661560240, 10.79108189686412622 ) ) ;
#69323=ORIENTED_EDGE ( 'NONE', *, *, #79457, .F. ) ;
#69324=CARTESIAN_POINT ( 'NONE',  ( 2.999999999999990674, 4.552185695429124657, 5.000000000000000000 ) ) ;
#69326=AXIS2_PLACEMENT_3D ( 'NONE', #85388, #96950, #141200 ) ;
#69328=DIRECTION ( 'NONE',  ( 0.3543493200069162685, -0.000000000000000000, -0.9351131265310288487 ) ) ;
#69331=CARTESIAN_POINT ( 'NONE',  ( 3.707106781186513711, -18.74070752338409562, 5.000000000000000000 ) ) ;
#69333=EDGE_LOOP ( 'NONE', ( #6963, #43769, #36691, #72018 ) ) ;
#69334=VECTOR ( 'NONE', #107536, 1000.000000000000000 ) ;
#69335=CARTESIAN_POINT ( 'NONE',  ( 19.11017322888197612, -22.22500000000000142, 4.785647885939352975 ) ) ;
#69336=ORIENTED_EDGE ( 'NONE', *, *, #111430, .F. ) ;
#69337=ORIENTED_EDGE ( 'NONE', *, *, #51814, .F. ) ;
#69339=EDGE_CURVE ( 'NONE', #128957, #119015, #17886, .T. ) ;
#69340=PLANE ( 'NONE',  #125766 ) ;
#69341=VECTOR ( 'NONE', #65539, 999.9999999999998863 ) ;
#69345=DIRECTION ( 'NONE',  ( -0.7071067811865486830, -0.7071067811865464625, 0.000000000000000000 ) ) ;
#69346=PLANE ( 'NONE',  #122665 ) ;
#69347=ADVANCED_FACE ( 'NONE', ( #62160 ), #106325, .F. ) ;
#69349=DIRECTION ( 'NONE',  ( 1.000000000000000000, 0.000000000000000000, 0.000000000000000000 ) ) ;
#69350=VERTEX_POINT ( 'NONE', #20047 ) ;
#69352=AXIS2_PLACEMENT_3D ( 'NONE', #828, #142951, #99423 ) ;
#69353=DIRECTION ( 'NONE',  ( 0.7071067811865486830, -0.7071067811865464625, -0.000000000000000000 ) ) ;
#69354=EDGE_CURVE ( 'NONE', #94828, #41854, #141117, .T. ) ;
#69355=EDGE_CURVE ( 'NONE', #28440, #62795, #87477, .T. ) ;
#69358=EDGE_CURVE ( 'NONE', #19458, #71456, #119353, .T. ) ;
#69359=PLANE ( 'NONE',  #133974 ) ;
#69362=ORIENTED_EDGE ( 'NONE', *, *, #947, .T. ) ;
#69363=EDGE_CURVE ( 'NONE', #63037, #81871, #29498, .T. ) ;
#69364=ORIENTED_EDGE ( 'NONE', *, *, #25974, .T. ) ;
#69366=VECTOR ( 'NONE', #109842, 999.9999999999998863 ) ;
#69368=FACE_OUTER_BOUND ( 'NONE', #64474, .T. ) ;
#69369=LINE ( 'NONE', #114277, #122310 ) ;
#69370=CARTESIAN_POINT ( 'NONE',  ( -0.8748538069076501333, -14.24070752338413826, 9.401115078912660294 ) ) ;
#69371=ADVANCED_FACE ( 'NONE', ( #97612 ), #109215, .T. ) ;
#69373=CARTESIAN_POINT ( 'NONE',  ( 14.99999999999989164, -7.068876922607732816, 4.000000000000000000 ) ) ;
#69374=CARTESIAN_POINT ( 'NONE',  ( -18.29974487139159223, -27.71228299555219010, 4.000000000000000000 ) ) ;
#69375=DIRECTION ( 'NONE',  ( 0.7071067811865487940, 0.7071067811865463515, -0.000000000000000000 ) ) ;
#69376=LINE ( 'NONE', #36717, #67361 ) ;
#69377=ORIENTED_EDGE ( 'NONE', *, *, #13778, .F. ) ;
#69379=EDGE_LOOP ( 'NONE', ( #12511, #63722, #59989, #93464 ) ) ;
#69380=EDGE_CURVE ( 'NONE', #94753, #77993, #9894, .T. ) ;
#69382=EDGE_LOOP ( 'NONE', ( #30738, #117358, #71546, #120282 ) ) ;
#69383=LINE ( 'NONE', #78113, #94905 ) ;
#69384=CARTESIAN_POINT ( 'NONE',  ( 12.79289321881337216, -5.240707523384223521, 5.000000000000000000 ) ) ;
#69387=VERTEX_POINT ( 'NONE', #130280 ) ;
#69388=DIRECTION ( 'NONE',  ( -0.000000000000000000, 0.000000000000000000, 1.000000000000000000 ) ) ;
#69389=ORIENTED_EDGE ( 'NONE', *, *, #107346, .T. ) ;
#69391=CARTESIAN_POINT ( 'NONE',  ( 18.18398860626898994, 28.73617430169800002, 5.000000000000000000 ) ) ;
#69394=DIRECTION ( 'NONE',  ( -0.7071067811865487940, 0.7071067811865463515, -0.000000000000000000 ) ) ;
#69395=ORIENTED_EDGE ( 'NONE', *, *, #48236, .F. ) ;
#69396=CARTESIAN_POINT ( 'NONE',  ( 30.83652871126530570, 15.75929247661555443, 9.299976744542991725 ) ) ;
#69397=LINE ( 'NONE', #1928, #3252 ) ;
#69398=PLANE ( 'NONE',  #15999 ) ;
#69401=FACE_OUTER_BOUND ( 'NONE', #64286, .T. ) ;
#69403=ORIENTED_EDGE ( 'NONE', *, *, #45463, .F. ) ;
#69404=CARTESIAN_POINT ( 'NONE',  ( 5.816011393731002066, 28.73617430169783304, 5.000000000000000000 ) ) ;
#69406=VERTEX_POINT ( 'NONE', #107069 ) ;
#69408=ADVANCED_FACE ( 'NONE', ( #30969 ), #31667, .F. ) ;
#69409=FACE_OUTER_BOUND ( 'NONE', #106002, .T. ) ;
#69410=DIRECTION ( 'NONE',  ( 0.7071067811865486830, -0.7071067811865464625, -0.000000000000000000 ) ) ;
#69411=VECTOR ( 'NONE', #1650, 1000.000000000000000 ) ;
#69412=LINE ( 'NONE', #13556, #46990 ) ;
#69414=ORIENTED_EDGE ( 'NONE', *, *, #42204, .F. ) ;
#69417=AXIS2_PLACEMENT_3D ( 'NONE', #112575, #3091, #124164 ) ;
#69418=CARTESIAN_POINT ( 'NONE',  ( 2.292893218813447209, -6.740707523384214639, 5.000000000000000000 ) ) ;
#69419=ADVANCED_FACE ( 'NONE', ( #63608 ), #108456, .F. ) ;
#69420=AXIS2_PLACEMENT_3D ( 'NONE', #6661, #59691, #27745 ) ;
#69421=CARTESIAN_POINT ( 'NONE',  ( 39.48921356237310221, -27.52281430457082934, 5.000000000000000000 ) ) ;
#69423=DIRECTION ( 'NONE',  ( -0.6830127018922181881, 0.6830127018922202975, -0.2588190451025214056 ) ) ;
#69424=CARTESIAN_POINT ( 'NONE',  ( 6.938893903907228378E-15, 4.552185695429122880, 5.000000000000000000 ) ) ;
#69426=EDGE_LOOP ( 'NONE', ( #133158, #117054, #34149, #81227 ) ) ;
#69427=CARTESIAN_POINT ( 'NONE',  ( 42.18398860626899705, 28.73617430169816700, 5.000000000000000000 ) ) ;
#69428=LINE ( 'NONE', #3408, #137842 ) ;
#69429=LINE ( 'NONE', #79632, #60926 ) ;
#69430=CARTESIAN_POINT ( 'NONE',  ( -10.49999999999992184, -13.91253812416061031, 4.000000000000000000 ) ) ;
#69433=ORIENTED_EDGE ( 'NONE', *, *, #60846, .T. ) ;
#69434=VERTEX_POINT ( 'NONE', #85301 ) ;
#69436=VECTOR ( 'NONE', #81130, 1000.000000000000000 ) ;
#69437=VERTEX_POINT ( 'NONE', #129524 ) ;
#69439=DIRECTION ( 'NONE',  ( 0.7071067811865486830, -0.7071067811865464625, -0.000000000000000000 ) ) ;
#69440=CARTESIAN_POINT ( 'NONE',  ( -29.99999999999979394, 4.965500833774300737, -4.007596771432589300 ) ) ;
#69441=DIRECTION ( 'NONE',  ( -0.6830127018922180770, -0.6830127018922204085, -0.2588190451025213501 ) ) ;
#69442=PLANE ( 'NONE',  #13299 ) ;
#69443=VERTEX_POINT ( 'NONE', #64293 ) ;
#69444=PLANE ( 'NONE',  #116214 ) ;
#69445=DIRECTION ( 'NONE',  ( -0.6830127018922181881, 0.6830127018922202975, -0.2588190451025214056 ) ) ;
#69446=CARTESIAN_POINT ( 'NONE',  ( -4.499999999999968914, -15.29013452822854724, 0.3645803511610244962 ) ) ;
#69447=VECTOR ( 'NONE', #65875, 1000.000000000000000 ) ;
#69450=EDGE_CURVE ( 'NONE', #130548, #63481, #53409, .T. ) ;
#69451=LINE ( 'NONE', #70195, #139302 ) ;
#69452=FACE_OUTER_BOUND ( 'NONE', #124905, .T. ) ;
#69453=PLANE ( 'NONE',  #125659 ) ;
#69454=AXIS2_PLACEMENT_3D ( 'NONE', #30170, #74419, #8382 ) ;
#69455=VECTOR ( 'NONE', #9437, 1000.000000000000000 ) ;
#69457=ORIENTED_EDGE ( 'NONE', *, *, #143270, .F. ) ;
#69458=EDGE_CURVE ( 'NONE', #137730, #71992, #45426, .T. ) ;
#69459=LINE ( 'NONE', #110762, #21361 ) ;
#69460=VECTOR ( 'NONE', #2717, 1000.000000000000000 ) ;
#69461=LINE ( 'NONE', #14341, #84805 ) ;
#69464=LINE ( 'NONE', #15038, #16466 ) ;
#69465=VECTOR ( 'NONE', #45360, 999.9999999999998863 ) ;
#69466=PLANE ( 'NONE',  #43338 ) ;
#69467=CARTESIAN_POINT ( 'NONE',  ( -54.18398860626899705, 28.73617430169825226, 5.000000000000000000 ) ) ;
#69469=EDGE_CURVE ( 'NONE', #26613, #68002, #33133, .T. ) ;
#69470=ORIENTED_EDGE ( 'NONE', *, *, #111428, .T. ) ;
#69472=DIRECTION ( 'NONE',  ( -0.7071067811865487940, 0.7071067811865463515, 0.000000000000000000 ) ) ;
#69473=ORIENTED_EDGE ( 'NONE', *, *, #6210, .T. ) ;
#69474=VERTEX_POINT ( 'NONE', #112092 ) ;
#69475=VECTOR ( 'NONE', #99482, 999.9999999999998863 ) ;
#69476=ADVANCED_FACE ( 'NONE', ( #67906 ), #112783, .F. ) ;
#69479=ORIENTED_EDGE ( 'NONE', *, *, #106544, .F. ) ;
#69481=CARTESIAN_POINT ( 'NONE',  ( -66.29974487139159578, -27.71228299555252406, 4.000000000000000000 ) ) ;
#69482=DIRECTION ( 'NONE',  ( -0.7071067811865486830, -0.7071067811865464625, 0.000000000000000000 ) ) ;
#69483=DIRECTION ( 'NONE',  ( -0.000000000000000000, 0.3543493200069153248, 0.9351131265310292928 ) ) ;
#69484=AXIS2_PLACEMENT_3D ( 'NONE', #69152, #133683, #110464 ) ;
#69485=FACE_OUTER_BOUND ( 'NONE', #44729, .T. ) ;
#69486=EDGE_LOOP ( 'NONE', ( #139391, #77066, #24787, #4178 ) ) ;
#69487=CARTESIAN_POINT ( 'NONE',  ( -5.994519915287488843, 28.92564299267942118, 4.000000000000000000 ) ) ;
#69488=CYLINDRICAL_SURFACE ( 'NONE', #41860, 0.5000000000000004441 ) ;
#69489=ORIENTED_EDGE ( 'NONE', *, *, #51359, .F. ) ;
#69490=DIRECTION ( 'NONE',  ( 1.000000000000000000, 0.000000000000000000, 0.000000000000000000 ) ) ;
#69492=EDGE_CURVE ( 'NONE', #55910, #68587, #22186, .T. ) ;
#69493=ORIENTED_EDGE ( 'NONE', *, *, #74634, .F. ) ;
#69494=DIRECTION ( 'NONE',  ( -0.6830127018922181881, 0.6830127018922202975, -0.2588190451025214056 ) ) ;
#69495=ORIENTED_EDGE ( 'NONE', *, *, #43746, .T. ) ;
#69496=VERTEX_POINT ( 'NONE', #1144 ) ;
#69497=DIRECTION ( 'NONE',  ( -0.7071067811865487940, 0.7071067811865463515, -0.000000000000000000 ) ) ;
#69499=EDGE_LOOP ( 'NONE', ( #112236, #13465, #14506, #100162 ) ) ;
#69500=VECTOR ( 'NONE', #37055, 1000.000000000000000 ) ;
#69501=DIRECTION ( 'NONE',  ( -0.6830127018922181881, 0.6830127018922202975, -0.2588190451025214056 ) ) ;
#69502=LINE ( 'NONE', #45618, #72793 ) ;
#69504=DIRECTION ( 'NONE',  ( -0.7071067811865487940, 0.7071067811865463515, 0.000000000000000000 ) ) ;
#69505=LINE ( 'NONE', #15753, #131549 ) ;
#69507=DIRECTION ( 'NONE',  ( -0.7071067811865487940, 0.7071067811865463515, -0.000000000000000000 ) ) ;
#69511=AXIS2_PLACEMENT_3D ( 'NONE', #115816, #60810, #104970 ) ;
#69512=ORIENTED_EDGE ( 'NONE', *, *, #140363, .F. ) ;
#69513=DIRECTION ( 'NONE',  ( -0.6830127018922181881, 0.6830127018922202975, -0.2588190451025214056 ) ) ;
#69514=VERTEX_POINT ( 'NONE', #44730 ) ;
#69515=ORIENTED_EDGE ( 'NONE', *, *, #133037, .F. ) ;
#69516=DIRECTION ( 'NONE',  ( 0.6830127018922181881, 0.6830127018922202975, -0.2588190451025214056 ) ) ;
#69518=AXIS2_PLACEMENT_3D ( 'NONE', #142810, #32640, #87000 ) ;
#69519=ORIENTED_EDGE ( 'NONE', *, *, #57006, .T. ) ;
#69520=AXIS2_PLACEMENT_3D ( 'NONE', #104440, #5821, #117445 ) ;
#69522=AXIS2_PLACEMENT_3D ( 'NONE', #70933, #121872, #91938 ) ;
#69523=DIRECTION ( 'NONE',  ( -0.000000000000000000, 0.000000000000000000, 1.000000000000000000 ) ) ;
#69524=CARTESIAN_POINT ( 'NONE',  ( 51.29974487139158867, -27.71228299555242103, 4.000000000000000000 ) ) ;
#69525=CARTESIAN_POINT ( 'NONE',  ( 8.700255128608413102, -27.71228299555199825, 4.000000000000000000 ) ) ;
#69526=DIRECTION ( 'NONE',  ( 0.7071067811865487940, 0.7071067811865463515, 0.000000000000000000 ) ) ;
#69527=LINE ( 'NONE', #102146, #139041 ) ;
#69528=ADVANCED_FACE ( 'NONE', ( #102645 ), #88924, .F. ) ;
#69529=EDGE_LOOP ( 'NONE', ( #74866, #74167, #104266, #88029 ) ) ;
#69530=DIRECTION ( 'NONE',  ( -0.7071067811865486830, -0.7071067811865464625, 0.000000000000000000 ) ) ;
#69531=AXIS2_PLACEMENT_3D ( 'NONE', #61405, #28018, #125185 ) ;
#69532=VERTEX_POINT ( 'NONE', #34515 ) ;
#69534=ADVANCED_FACE ( 'NONE', ( #46131 ), #88194, .F. ) ;
#69536=ORIENTED_EDGE ( 'NONE', *, *, #105688, .T. ) ;
#69537=EDGE_CURVE ( 'NONE', #93801, #123539, #56318, .T. ) ;
#69540=ORIENTED_EDGE ( 'NONE', *, *, #136558, .F. ) ;
#69541=ORIENTED_EDGE ( 'NONE', *, *, #113763, .T. ) ;
#69542=EDGE_CURVE ( 'NONE', #39180, #35044, #42442, .T. ) ;
#69544=CARTESIAN_POINT ( 'NONE',  ( 35.99451991528749772, 28.92564299267963079, 4.000000000000000000 ) ) ;
#69546=DIRECTION ( 'NONE',  ( -0.7071067811865486830, -0.7071067811865464625, 0.000000000000000000 ) ) ;
#69547=DIRECTION ( 'NONE',  ( -0.7071067811865486830, -0.7071067811865464625, 0.000000000000000000 ) ) ;
#69548=EDGE_CURVE ( 'NONE', #9933, #86313, #110615, .T. ) ;
#69549=CARTESIAN_POINT ( 'NONE',  ( -12.48921356237309155, -27.52281430457064104, 5.000000000000000000 ) ) ;
#69550=ORIENTED_EDGE ( 'NONE', *, *, #99233, .T. ) ;
#69551=FACE_OUTER_BOUND ( 'NONE', #108078, .T. ) ;
#69552=LINE ( 'NONE', #113739, #80443 ) ;
#69553=AXIS2_PLACEMENT_3D ( 'NONE', #33774, #35919, #69247 ) ;
#69554=AXIS2_PLACEMENT_3D ( 'NONE', #35080, #48084, #69128 ) ;
#69556=CARTESIAN_POINT ( 'NONE',  ( -2.816011393730999401, 28.73617430169785436, 5.000000000000000000 ) ) ;
#69557=CARTESIAN_POINT ( 'NONE',  ( 63.48921356237309510, -27.52281430457099631, 5.000000000000000000 ) ) ;
#69558=VECTOR ( 'NONE', #7490, 1000.000000000000227 ) ;
#69560=FACE_OUTER_BOUND ( 'NONE', #38019, .T. ) ;
#69562=ORIENTED_EDGE ( 'NONE', *, *, #128574, .T. ) ;
#69563=EDGE_CURVE ( 'NONE', #120482, #138203, #68594, .T. ) ;
#69565=ORIENTED_EDGE ( 'NONE', *, *, #142705, .T. ) ;
#69566=EDGE_LOOP ( 'NONE', ( #84657, #121277, #44585, #9984 ) ) ;
#69567=EDGE_CURVE ( 'NONE', #2398, #81201, #33819, .T. ) ;
#69569=CARTESIAN_POINT ( 'NONE',  ( -3.461603553705685954, -9.740707523384180888, 17.74957260769609846 ) ) ;
#69570=CARTESIAN_POINT ( 'NONE',  ( 39.18398860626899705, 28.73617430169814568, 5.000000000000000000 ) ) ;
#69574=ORIENTED_EDGE ( 'NONE', *, *, #21580, .F. ) ;
#69576=CARTESIAN_POINT ( 'NONE',  ( -39.18398860626899705, 28.73617430169814568, 5.000000000000000000 ) ) ;
#69577=DIRECTION ( 'NONE',  ( 1.000000000000000000, 0.000000000000000000, 0.000000000000000000 ) ) ;
#69578=DIRECTION ( 'NONE',  ( 0.6830127018922180770, -0.6830127018922204085, -0.2588190451025213501 ) ) ;
#69579=AXIS2_PLACEMENT_3D ( 'NONE', #90129, #67715, #101002 ) ;
#69580=CARTESIAN_POINT ( 'NONE',  ( -1.828169399223514624, 15.75929247661555443, 4.000000000000000000 ) ) ;
#69581=DIRECTION ( 'NONE',  ( -0.6830127018922181881, 0.6830127018922202975, -0.2588190451025214056 ) ) ;
#69582=CARTESIAN_POINT ( 'NONE',  ( -17.27718569542927796, -21.72500000000000142, 5.000000000000000000 ) ) ;
#69585=AXIS2_PLACEMENT_3D ( 'NONE', #15163, #24630, #37679 ) ;
#69587=CARTESIAN_POINT ( 'NONE',  ( 25.49999999999982947, 16.18958161055405753, -11.56426086740805559 ) ) ;
#69588=CARTESIAN_POINT ( 'NONE',  ( 31.49999999999977973, -16.53360074219757081, 5.000000000000000000 ) ) ;
#69589=PLANE ( 'NONE',  #22307 ) ;
#69590=VERTEX_POINT ( 'NONE', #101911 ) ;
#69594=ORIENTED_EDGE ( 'NONE', *, *, #80528, .T. ) ;
#69595=ORIENTED_EDGE ( 'NONE', *, *, #121411, .F. ) ;
#69597=LINE ( 'NONE', #70330, #78078 ) ;
#69598=LINE ( 'NONE', #49971, #94948 ) ;
#69599=VECTOR ( 'NONE', #71842, 1000.000000000000227 ) ;
#69602=CARTESIAN_POINT ( 'NONE',  ( -25.49999999999982236, -1.533600742197719580, 5.000000000000000000 ) ) ;
#69603=DIRECTION ( 'NONE',  ( 0.3543493200069162685, -0.000000000000000000, -0.9351131265310288487 ) ) ;
#69604=PLANE ( 'NONE',  #18558 ) ;
#69607=CARTESIAN_POINT ( 'NONE',  ( -25.17183060077629619, 15.75929247661555976, 4.000000000000000000 ) ) ;
#69608=CARTESIAN_POINT ( 'NONE',  ( -9.707106781186471522, -12.74070752338415602, 5.000000000000000000 ) ) ;
#69609=CARTESIAN_POINT ( 'NONE',  ( 48.48921356237309510, -27.52281430457089328, 5.000000000000000000 ) ) ;
#69612=DIRECTION ( 'NONE',  ( -0.000000000000000000, 0.3543493200069153248, 0.9351131265310292928 ) ) ;
#69614=VECTOR ( 'NONE', #88436, 1000.000000000000000 ) ;
#69615=DIRECTION ( 'NONE',  ( 1.000000000000000000, -0.000000000000000000, 0.000000000000000000 ) ) ;
#69616=CARTESIAN_POINT ( 'NONE',  ( 42.18398860626899705, 28.73617430169816700, 5.000000000000000000 ) ) ;
#69618=VERTEX_POINT ( 'NONE', #16292 ) ;
#69620=ORIENTED_EDGE ( 'NONE', *, *, #60045, .F. ) ;
#69621=ADVANCED_FACE ( 'NONE', ( #3292 ), #5424, .F. ) ;
#69622=DIRECTION ( 'NONE',  ( 0.000000000000000000, -1.000000000000000000, 0.000000000000000000 ) ) ;
#69623=CARTESIAN_POINT ( 'NONE',  ( 18.18398860626898994, 28.73617430169800002, 5.000000000000000000 ) ) ;
#69624=VECTOR ( 'NONE', #130902, 1000.000000000000000 ) ;
#69625=LINE ( 'NONE', #60164, #83757 ) ;
#69626=DIRECTION ( 'NONE',  ( -0.7071067811865486830, -0.7071067811865464625, -0.000000000000000000 ) ) ;
#69627=VECTOR ( 'NONE', #95652, 1000.000000000000000 ) ;
#69629=EDGE_LOOP ( 'NONE', ( #69323, #114144, #83022, #105121 ) ) ;
#69630=EDGE_CURVE ( 'NONE', #58576, #82619, #27916, .T. ) ;
#69631=ORIENTED_EDGE ( 'NONE', *, *, #36800, .T. ) ;
#69633=VECTOR ( 'NONE', #26200, 1000.000000000000000 ) ;
#69634=VECTOR ( 'NONE', #57088, 1000.000000000000000 ) ;
#69635=VECTOR ( 'NONE', #55453, 1000.000000000000000 ) ;
#69637=VECTOR ( 'NONE', #19211, 1000.000000000000227 ) ;
#69638=ORIENTED_EDGE ( 'NONE', *, *, #114239, .F. ) ;
#69639=ORIENTED_EDGE ( 'NONE', *, *, #136940, .F. ) ;
#69641=VERTEX_POINT ( 'NONE', #38802 ) ;
#69642=PLANE ( 'NONE',  #60733 ) ;
#69644=AXIS2_PLACEMENT_3D ( 'NONE', #31778, #96274, #31080 ) ;
#69645=VERTEX_POINT ( 'NONE', #114887 ) ;
#69646=VERTEX_POINT ( 'NONE', #6119 ) ;
#69647=CARTESIAN_POINT ( 'NONE',  ( -26.27718569542921401, -21.72499999999999432, 5.000000000000000000 ) ) ;
#69648=ORIENTED_EDGE ( 'NONE', *, *, #38603, .T. ) ;
#69649=ORIENTED_EDGE ( 'NONE', *, *, #38469, .T. ) ;
#69650=AXIS2_PLACEMENT_3D ( 'NONE', #52593, #85213, #19957 ) ;
#69651=CARTESIAN_POINT ( 'NONE',  ( -6.489213562373093325, -27.52281430457059841, 5.000000000000000000 ) ) ;
#69652=VECTOR ( 'NONE', #137904, 999.9999999999998863 ) ;
#69653=VECTOR ( 'NONE', #132930, 1000.000000000000000 ) ;
#69654=DIRECTION ( 'NONE',  ( 0.7071067811865487940, -0.7071067811865463515, 0.000000000000000000 ) ) ;
#69655=CARTESIAN_POINT ( 'NONE',  ( -17.99451991528748351, 28.92564299267950645, 4.000000000000000000 ) ) ;
#69657=ORIENTED_EDGE ( 'NONE', *, *, #84816, .T. ) ;
#69658=DIRECTION ( 'NONE',  ( -0.7071067811865486830, -0.7071067811865464625, 0.000000000000000000 ) ) ;
#69659=VECTOR ( 'NONE', #25509, 999.9999999999998863 ) ;
#69660=DIRECTION ( 'NONE',  ( 1.000000000000000000, 0.000000000000000000, 0.000000000000000000 ) ) ;
#69661=VECTOR ( 'NONE', #134455, 1000.000000000000227 ) ;
#69664=FACE_BOUND ( 'NONE', #56757, .T. ) ;
#69665=ORIENTED_EDGE ( 'NONE', *, *, #133971, .F. ) ;
#69666=PLANE ( 'NONE',  #136016 ) ;
#69667=CARTESIAN_POINT ( 'NONE',  ( 17.99999999999987566, -3.033600742197710254, 5.000000000000000000 ) ) ;
#69669=CARTESIAN_POINT ( 'NONE',  ( -23.29289321881329045, -9.740707523384187994, 5.000000000000000000 ) ) ;
#69670=EDGE_CURVE ( 'NONE', #108960, #118884, #46139, .T. ) ;
#69671=ORIENTED_EDGE ( 'NONE', *, *, #101575, .T. ) ;
#69672=DIRECTION ( 'NONE',  ( 0.3543493200069163240, 0.000000000000000000, -0.9351131265310288487 ) ) ;
#69674=ORIENTED_EDGE ( 'NONE', *, *, #54876, .T. ) ;
#69675=ORIENTED_EDGE ( 'NONE', *, *, #112062, .F. ) ;
#69681=CARTESIAN_POINT ( 'NONE',  ( -38.99451991528749062, 28.92564299267965211, 4.000000000000000000 ) ) ;
#69682=LINE ( 'NONE', #24010, #128470 ) ;
#69683=ORIENTED_EDGE ( 'NONE', *, *, #118062, .T. ) ;
#69685=VECTOR ( 'NONE', #10537, 1000.000000000000000 ) ;
#69688=DIRECTION ( 'NONE',  ( -0.000000000000000000, -0.3543493200069152693, 0.9351131265310292928 ) ) ;
#69691=LINE ( 'NONE', #23270, #66828 ) ;
#69693=VERTEX_POINT ( 'NONE', #49704 ) ;
#69695=ORIENTED_EDGE ( 'NONE', *, *, #89367, .T. ) ;
#69697=EDGE_LOOP ( 'NONE', ( #14869, #137078, #30397, #45755 ) ) ;
#69699=VERTEX_POINT ( 'NONE', #4675 ) ;
#69700=CARTESIAN_POINT ( 'NONE',  ( -8.816011393731004731, 28.73617430169781173, 5.000000000000000000 ) ) ;
#69701=PLANE ( 'NONE',  #76335 ) ;
#69702=ORIENTED_EDGE ( 'NONE', *, *, #29253, .F. ) ;
#69703=CARTESIAN_POINT ( 'NONE',  ( 16.49999999999988631, -2.947814304570806065, 5.000000000000000000 ) ) ;
#69704=VECTOR ( 'NONE', #62452, 1000.000000000000000 ) ;
#69705=EDGE_LOOP ( 'NONE', ( #47650, #142722, #11023, #95654 ) ) ;
#69708=CARTESIAN_POINT ( 'NONE',  ( -7.499999999999943157, -13.91253812416061386, 4.000000000000000000 ) ) ;
#69709=EDGE_CURVE ( 'NONE', #129523, #69972, #26497, .T. ) ;
#69711=ORIENTED_EDGE ( 'NONE', *, *, #143542, .T. ) ;
#69713=CARTESIAN_POINT ( 'NONE',  ( 2.999999999999985345, 11.58746187583912324, 4.000000000000000000 ) ) ;
#69714=EDGE_CURVE ( 'NONE', #83476, #86617, #39533, .T. ) ;
#69715=CARTESIAN_POINT ( 'NONE',  ( -0.4892135623730947680, -27.52281430457055578, 5.000000000000000000 ) ) ;
#69716=DIRECTION ( 'NONE',  ( -0.6830127018922180770, -0.6830127018922204085, -0.2588190451025213501 ) ) ;
#69717=EDGE_LOOP ( 'NONE', ( #9399, #16673, #91698, #8175 ) ) ;
#69718=FILL_AREA_STYLE_COLOUR ( '', #114424 ) ;
#69719=ORIENTED_EDGE ( 'NONE', *, *, #82956, .F. ) ;
#69721=LINE ( 'NONE', #16729, #25472 ) ;
#69722=LINE ( 'NONE', #15977, #3375 ) ;
#69723=VECTOR ( 'NONE', #139059, 1000.000000000000000 ) ;
#69725=EDGE_CURVE ( 'NONE', #134832, #60397, #125087, .T. ) ;
#69726=EDGE_CURVE ( 'NONE', #96542, #92295, #15566, .T. ) ;
#69727=ORIENTED_EDGE ( 'NONE', *, *, #11788, .F. ) ;
#69728=VECTOR ( 'NONE', #38813, 1000.000000000000000 ) ;
#69729=CARTESIAN_POINT ( 'NONE',  ( -18.00548008471250583, 28.92564299267925776, 4.000000000000000000 ) ) ;
#69730=AXIS2_PLACEMENT_3D ( 'NONE', #4110, #89754, #136114 ) ;
#69731=CARTESIAN_POINT ( 'NONE',  ( -2.999999999999975131, -6.412538124160689357, 4.000000000000000000 ) ) ;
#69732=CARTESIAN_POINT ( 'NONE',  ( 18.48921356237309510, -27.52281430457068367, 5.000000000000000000 ) ) ;
#69733=EDGE_LOOP ( 'NONE', ( #14437, #42941, #511, #107307 ) ) ;
#69734=LINE ( 'NONE', #136373, #9610 ) ;
#69736=VECTOR ( 'NONE', #130536, 1000.000000000000000 ) ;
#69737=VECTOR ( 'NONE', #78900, 1000.000000000000114 ) ;
#69738=PLANE ( 'NONE',  #46976 ) ;
#69739=VECTOR ( 'NONE', #121894, 1000.000000000000000 ) ;
#69740=VERTEX_POINT ( 'NONE', #70742 ) ;
#69741=EDGE_CURVE ( 'NONE', #38431, #23319, #80889, .T. ) ;
#69742=FACE_OUTER_BOUND ( 'NONE', #68451, .T. ) ;
#69743=ORIENTED_EDGE ( 'NONE', *, *, #4569, .F. ) ;
#69744=ADVANCED_FACE ( 'NONE', ( #47578 ), #138113, .F. ) ;
#69745=VERTEX_POINT ( 'NONE', #138836 ) ;
#69747=AXIS2_PLACEMENT_3D ( 'NONE', #52627, #96819, #32329 ) ;
#69748=DIRECTION ( 'NONE',  ( 0.6830127018922180770, -0.6830127018922204085, -0.2588190451025213501 ) ) ;
#69749=ORIENTED_EDGE ( 'NONE', *, *, #40631, .T. ) ;
#69750=EDGE_CURVE ( 'NONE', #11057, #47805, #82318, .T. ) ;
#69752=VERTEX_POINT ( 'NONE', #93881 ) ;
#69753=AXIS2_PLACEMENT_3D ( 'NONE', #17043, #83756, #107607 ) ;
#69755=DIRECTION ( 'NONE',  ( -0.3543493200069163240, -0.000000000000000000, 0.9351131265310288487 ) ) ;
#69756=FACE_OUTER_BOUND ( 'NONE', #125916, .T. ) ;
#69758=VECTOR ( 'NONE', #80790, 999.9999999999998863 ) ;
#69759=EDGE_CURVE ( 'NONE', #11112, #39875, #27191, .T. ) ;
#69760=CARTESIAN_POINT ( 'NONE',  ( -39.29974487139159578, -27.71228299555233576, 4.000000000000000000 ) ) ;
#69761=DIRECTION ( 'NONE',  ( 0.3543493200069162685, -0.000000000000000000, -0.9351131265310288487 ) ) ;
#69762=DIRECTION ( 'NONE',  ( 0.6830127018922181881, 0.6830127018922202975, -0.2588190451025214056 ) ) ;
#69763=DIRECTION ( 'NONE',  ( -0.6830127018922181881, 0.6830127018922202975, -0.2588190451025214056 ) ) ;
#69766=ORIENTED_EDGE ( 'NONE', *, *, #103845, .T. ) ;
#69767=VERTEX_POINT ( 'NONE', #17725 ) ;
#69769=VECTOR ( 'NONE', #11799, 1000.000000000000227 ) ;
#69770=VERTEX_POINT ( 'NONE', #103314 ) ;
#69771=ORIENTED_EDGE ( 'NONE', *, *, #3777, .T. ) ;
#69773=ORIENTED_EDGE ( 'NONE', *, *, #137841, .F. ) ;
#69774=ADVANCED_FACE ( 'NONE', ( #3965 ), #104764, .T. ) ;
#69775=DIRECTION ( 'NONE',  ( 0.7071067811865487940, -0.7071067811865463515, 0.000000000000000000 ) ) ;
#69776=CARTESIAN_POINT ( 'NONE',  ( 5.994519915287488843, 28.92564299267942118, 4.000000000000000000 ) ) ;
#69777=VECTOR ( 'NONE', #100915, 1000.000000000000000 ) ;
#69778=ORIENTED_EDGE ( 'NONE', *, *, #105102, .F. ) ;
#69779=LINE ( 'NONE', #134293, #104062 ) ;
#69780=CARTESIAN_POINT ( 'NONE',  ( 33.29974487139158867, -27.71228299555229313, 4.000000000000000000 ) ) ;
#69781=DIRECTION ( 'NONE',  ( -0.000000000000000000, -0.000000000000000000, 1.000000000000000000 ) ) ;
#69783=VECTOR ( 'NONE', #138550, 1000.000000000000000 ) ;
#69784=ORIENTED_EDGE ( 'NONE', *, *, #55759, .F. ) ;
#69785=CARTESIAN_POINT ( 'NONE',  ( 9.489213562373095101, -27.52281430457062328, 5.000000000000000000 ) ) ;
#69787=LINE ( 'NONE', #26947, #112244 ) ;
#69788=DIRECTION ( 'NONE',  ( -0.7071067811865487940, 0.7071067811865463515, -0.000000000000000000 ) ) ;
#69789=CARTESIAN_POINT ( 'NONE',  ( 0.000000000000000000, 0.000000000000000000, 5.000000000000000000 ) ) ;
#69790=CARTESIAN_POINT ( 'NONE',  ( 3.183988606268992161, 28.73617430169789699, 5.000000000000000000 ) ) ;
#69792=EDGE_CURVE ( 'NONE', #68883, #73190, #107610, .T. ) ;
#69793=DIRECTION ( 'NONE',  ( -0.7071067811865486830, -0.7071067811865464625, 0.000000000000000000 ) ) ;
#69794=CARTESIAN_POINT ( 'NONE',  ( -39.48921356237310221, -27.52281430457082934, 5.000000000000000000 ) ) ;
#69795=AXIS2_PLACEMENT_3D ( 'NONE', #118648, #22170, #101173 ) ;
#69796=VERTEX_POINT ( 'NONE', #52517 ) ;
#69797=ORIENTED_EDGE ( 'NONE', *, *, #82592, .T. ) ;
#69800=EDGE_LOOP ( 'NONE', ( #77523, #137248, #9552, #91319 ) ) ;
#69801=CARTESIAN_POINT ( 'NONE',  ( -8.510786437626906675, -27.52281430457049183, 5.000000000000000000 ) ) ;
#69802=AXIS2_PLACEMENT_3D ( 'NONE', #6230, #60710, #83880 ) ;
#69803=CARTESIAN_POINT ( 'NONE',  ( 27.48921356237309155, -27.52281430457074762, 5.000000000000000000 ) ) ;
#69804=ORIENTED_EDGE ( 'NONE', *, *, #86869, .F. ) ;
#69805=VECTOR ( 'NONE', #50295, 1000.000000000000227 ) ;
#69806=CARTESIAN_POINT ( 'NONE',  ( -34.92500000000001137, 22.22500000000000142, 4.000000000000000000 ) ) ;
#69807=DIRECTION ( 'NONE',  ( 0.7071067811865487940, -0.7071067811865463515, 0.000000000000000000 ) ) ;
#69808=LINE ( 'NONE', #60343, #123060 ) ;
#69811=EDGE_CURVE ( 'NONE', #105583, #38928, #119889, .T. ) ;
#69812=PLANE ( 'NONE',  #82681 ) ;
#69813=ORIENTED_EDGE ( 'NONE', *, *, #71350, .T. ) ;
#69814=AXIS2_PLACEMENT_3D ( 'NONE', #122098, #19932, #11908 ) ;
#69816=CARTESIAN_POINT ( 'NONE',  ( 33.79289321881321939, 12.75929247661558819, 5.000000000000000000 ) ) ;
#69817=PLANE ( 'NONE',  #16606 ) ;
#69818=LINE ( 'NONE', #103120, #115839 ) ;
#69820=EDGE_CURVE ( 'NONE', #27138, #17308, #118485, .T. ) ;
#69821=ORIENTED_EDGE ( 'NONE', *, *, #96338, .T. ) ;
#69822=CARTESIAN_POINT ( 'NONE',  ( 20.67183060077632462, -18.74070752338408852, 4.000000000000000000 ) ) ;
#69824=FACE_OUTER_BOUND ( 'NONE', #78137, .T. ) ;
#69825=FACE_OUTER_BOUND ( 'NONE', #138999, .T. ) ;
#69827=CARTESIAN_POINT ( 'NONE',  ( -33.48921356237309510, -27.52281430457078670, 5.000000000000000000 ) ) ;
#69828=LINE ( 'NONE', #92234, #31550 ) ;
#69829=ORIENTED_EDGE ( 'NONE', *, *, #100978, .T. ) ;
#69830=EDGE_CURVE ( 'NONE', #105472, #103136, #98181, .T. ) ;
#69831=ORIENTED_EDGE ( 'NONE', *, *, #135297, .T. ) ;
#69832=CARTESIAN_POINT ( 'NONE',  ( -17.99451991528748351, 28.92564299267950645, 4.000000000000000000 ) ) ;
#69833=VECTOR ( 'NONE', #27407, 999.9999999999998863 ) ;
#69834=ORIENTED_EDGE ( 'NONE', *, *, #132464, .F. ) ;
#69835=VECTOR ( 'NONE', #48815, 999.9999999999998863 ) ;
#69836=VECTOR ( 'NONE', #78016, 1000.000000000000000 ) ;
#69837=DIRECTION ( 'NONE',  ( 0.7071067811865487940, 0.7071067811865463515, 0.000000000000000000 ) ) ;
#69838=EDGE_CURVE ( 'NONE', #27882, #142853, #108290, .T. ) ;
#69839=ORIENTED_EDGE ( 'NONE', *, *, #73173, .F. ) ;
#69840=DIRECTION ( 'NONE',  ( -0.6830127018922180770, -0.6830127018922204085, -0.2588190451025213501 ) ) ;
#69842=VECTOR ( 'NONE', #25154, 999.9999999999998863 ) ;
#69844=VECTOR ( 'NONE', #48381, 999.9999999999998863 ) ;
#69845=CARTESIAN_POINT ( 'NONE',  ( -62.99451991528749772, 28.92564299267982264, 4.000000000000000000 ) ) ;
#69846=EDGE_CURVE ( 'NONE', #77053, #15867, #75717, .T. ) ;
#69847=FACE_BOUND ( 'NONE', #40844, .T. ) ;
#69848=CARTESIAN_POINT ( 'NONE',  ( 10.77149322861328073, 20.25929247661551358, 7.808871592221793279 ) ) ;
#69850=LINE ( 'NONE', #137220, #112799 ) ;
#69851=ADVANCED_FACE ( 'NONE', ( #109028 ), #64124, .T. ) ;
#69854=CYLINDRICAL_SURFACE ( 'NONE', #31948, 0.5000000000000004441 ) ;
#69855=ORIENTED_EDGE ( 'NONE', *, *, #132289, .F. ) ;
#69856=DIRECTION ( 'NONE',  ( -0.3543493200069162685, -0.000000000000000000, -0.9351131265310288487 ) ) ;
#69857=ORIENTED_EDGE ( 'NONE', *, *, #94078, .F. ) ;
#69858=ORIENTED_EDGE ( 'NONE', *, *, #118147, .T. ) ;
#69860=ORIENTED_EDGE ( 'NONE', *, *, #52155, .F. ) ;
#69861=EDGE_CURVE ( 'NONE', #132792, #31251, #21331, .T. ) ;
#69862=VECTOR ( 'NONE', #67721, 1000.000000000000227 ) ;
#69863=CARTESIAN_POINT ( 'NONE',  ( 3.489213562373097322, -27.52281430457057709, 5.000000000000000000 ) ) ;
#69864=VERTEX_POINT ( 'NONE', #130100 ) ;
#69865=DIRECTION ( 'NONE',  ( -0.3543493200069162685, -0.000000000000000000, -0.9351131265310288487 ) ) ;
#69866=ADVANCED_FACE ( 'NONE', ( #142411 ), #42394, .F. ) ;
#69869=AXIS2_PLACEMENT_3D ( 'NONE', #116501, #73709, #137553 ) ;
#69872=LINE ( 'NONE', #101017, #15745 ) ;
#69874=VECTOR ( 'NONE', #90334, 1000.000000000000000 ) ;
#69875=DIRECTION ( 'NONE',  ( -0.7071067811865486830, -0.7071067811865464625, 0.000000000000000000 ) ) ;
#69876=CARTESIAN_POINT ( 'NONE',  ( 78.18398860626899705, 28.73617430169841924, 5.000000000000000000 ) ) ;
#69877=ORIENTED_EDGE ( 'NONE', *, *, #130757, .F. ) ;
#69880=DIRECTION ( 'NONE',  ( -0.7071067811865486830, -0.7071067811865464625, -0.000000000000000000 ) ) ;
#69881=DIRECTION ( 'NONE',  ( -0.000000000000000000, 0.000000000000000000, 1.000000000000000000 ) ) ;
#69882=VERTEX_POINT ( 'NONE', #96702 ) ;
#69883=VERTEX_POINT ( 'NONE', #106892 ) ;
#69884=ORIENTED_EDGE ( 'NONE', *, *, #96017, .F. ) ;
#69887=VERTEX_POINT ( 'NONE', #140948 ) ;
#69888=CARTESIAN_POINT ( 'NONE',  ( 11.54939188068398259, -22.22500000000000142, -12.61088438758952535 ) ) ;
#69890=DIRECTION ( 'NONE',  ( 0.7071067811865487940, 0.7071067811865463515, 0.000000000000000000 ) ) ;
#69891=ADVANCED_FACE ( 'NONE', ( #43097 ), #97435, .F. ) ;
#69893=EDGE_CURVE ( 'NONE', #120153, #99498, #86603, .T. ) ;
#69894=DIRECTION ( 'NONE',  ( -0.000000000000000000, 0.000000000000000000, 1.000000000000000000 ) ) ;
#69895=ORIENTED_EDGE ( 'NONE', *, *, #43812, .T. ) ;
#69896=LINE ( 'NONE', #69157, #3978 ) ;
#69901=LINE ( 'NONE', #22740, #42630 ) ;
#69902=ORIENTED_EDGE ( 'NONE', *, *, #134725, .T. ) ;
#69903=AXIS2_PLACEMENT_3D ( 'NONE', #118371, #21213, #77056 ) ;
#69906=LINE ( 'NONE', #15436, #70153 ) ;
#69907=ADVANCED_FACE ( 'NONE', ( #96019 ), #84469, .F. ) ;
#69908=EDGE_CURVE ( 'NONE', #141201, #31209, #129359, .T. ) ;
#69909=LINE ( 'NONE', #59041, #116499 ) ;
#69910=EDGE_LOOP ( 'NONE', ( #103194, #139311, #84724 ) ) ;
#69912=FACE_OUTER_BOUND ( 'NONE', #25990, .T. ) ;
#69913=VECTOR ( 'NONE', #15080, 1000.000000000000227 ) ;
#69914=CARTESIAN_POINT ( 'NONE',  ( -17.93988928955969087, -9.740707523384180888, 10.89222023123385341 ) ) ;
#69915=DIRECTION ( 'NONE',  ( -0.7071067811865486830, -0.7071067811865464625, 0.000000000000000000 ) ) ;
#69917=EDGE_LOOP ( 'NONE', ( #102079, #55205, #77010, #76587 ) ) ;
#69918=LINE ( 'NONE', #136540, #11429 ) ;
#69919=EDGE_CURVE ( 'NONE', #64709, #36781, #30797, .T. ) ;
#69920=DIRECTION ( 'NONE',  ( -0.000000000000000000, -0.3543493200069152693, 0.9351131265310292928 ) ) ;
#69922=LINE ( 'NONE', #113361, #128113 ) ;
#69923=ADVANCED_FACE ( 'NONE', ( #111161 ), #102994, .F. ) ;
#69924=LINE ( 'NONE', #78618, #55291 ) ;
#69925=VERTEX_POINT ( 'NONE', #37754 ) ;
#69926=EDGE_CURVE ( 'NONE', #138697, #52621, #48613, .T. ) ;
#69927=ORIENTED_EDGE ( 'NONE', *, *, #37292, .T. ) ;
#69929=LINE ( 'NONE', #111976, #19240 ) ;
#69931=CARTESIAN_POINT ( 'NONE',  ( 4.171830600776443632, 9.759292476615621936, 4.000000000000000000 ) ) ;
#69932=ADVANCED_FACE ( 'NONE', ( #251 ), #126176, .T. ) ;
#69933=CARTESIAN_POINT ( 'NONE',  ( -32.99451991528749062, 28.92564299267960948, 4.000000000000000000 ) ) ;
#69934=CARTESIAN_POINT ( 'NONE',  ( -33.48921356237309510, -27.52281430457078670, 5.000000000000000000 ) ) ;
#69935=ADVANCED_FACE ( 'NONE', ( #81992 ), #65589, .F. ) ;
#69936=DIRECTION ( 'NONE',  ( -0.6830127018922180770, -0.6830127018922204085, -0.2588190451025213501 ) ) ;
#69937=EDGE_LOOP ( 'NONE', ( #53308, #88452, #47186, #60442, #72809 ) ) ;
#69938=LINE ( 'NONE', #79393, #129871 ) ;
#69939=CARTESIAN_POINT ( 'NONE',  ( -0.7070132642930445632, -21.74070752338405654, 4.999753212805222446 ) ) ;
#69940=VECTOR ( 'NONE', #121399, 1000.000000000000227 ) ;
#69941=EDGE_CURVE ( 'NONE', #60486, #70075, #22026, .T. ) ;
#69942=VECTOR ( 'NONE', #31181, 1000.000000000000000 ) ;
#69943=DIRECTION ( 'NONE',  ( -0.3543493200069163240, -0.000000000000000000, 0.9351131265310288487 ) ) ;
#69945=( BOUNDED_CURVE ( )  B_SPLINE_CURVE ( 3, ( #82845, #50213, #125636, #37920 ),
 .UNSPECIFIED., .F., .F. ) 
 B_SPLINE_CURVE_WITH_KNOTS ( ( 4, 4 ),
 ( 3.581556339957213897, 3.677360298529522176 ),
 .UNSPECIFIED. ) 
 CURVE ( )  GEOMETRIC_REPRESENTATION_ITEM ( )  RATIONAL_B_SPLINE_CURVE ( ( 1.000000000000000000, 0.9992352797041761381, 0.9992352797041761381, 1.000000000000000000 ) ) 
 REPRESENTATION_ITEM ( '' )  );
#69946=DIRECTION ( 'NONE',  ( 0.3543493200069162685, -0.000000000000000000, -0.9351131265310288487 ) ) ;
#69949=ORIENTED_EDGE ( 'NONE', *, *, #749, .T. ) ;
#69950=DIRECTION ( 'NONE',  ( 0.7071067811865487940, 0.7071067811865463515, 0.000000000000000000 ) ) ;
#69951=ORIENTED_EDGE ( 'NONE', *, *, #92415, .T. ) ;
#69952=AXIS2_PLACEMENT_3D ( 'NONE', #38038, #138773, #40195 ) ;
#69953=EDGE_CURVE ( 'NONE', #122015, #84039, #109758, .T. ) ;
#69954=AXIS2_PLACEMENT_3D ( 'NONE', #134652, #24433, #2663 ) ;
#69955=DIRECTION ( 'NONE',  ( -0.7071067811865487940, 0.7071067811865463515, 0.000000000000000000 ) ) ;
#69957=CARTESIAN_POINT ( 'NONE',  ( 66.29974487139159578, -27.71228299555252406, 4.000000000000000000 ) ) ;
#69958=DIRECTION ( 'NONE',  ( 0.6830127018922180770, -0.6830127018922204085, -0.2588190451025213501 ) ) ;
#69959=CARTESIAN_POINT ( 'NONE',  ( 54.48921356237310221, -27.52281430457093236, 5.000000000000000000 ) ) ;
#69962=VERTEX_POINT ( 'NONE', #10431 ) ;
#69963=VERTEX_POINT ( 'NONE', #59511 ) ;
#69964=DIRECTION ( 'NONE',  ( 0.7071067811865487940, 0.7071067811865463515, -0.000000000000000000 ) ) ;
#69965=CARTESIAN_POINT ( 'NONE',  ( 42.29974487139158157, -27.71228299555235708, 4.000000000000000000 ) ) ;
#69966=EDGE_CURVE ( 'NONE', #131683, #3009, #43797, .T. ) ;
#69967=PLANE ( 'NONE',  #3344 ) ;
#69968=DIRECTION ( 'NONE',  ( -0.7071067811865486830, -0.7071067811865464625, 0.000000000000000000 ) ) ;
#69970=ADVANCED_FACE ( 'NONE', ( #125465 ), #124739, .F. ) ;
#69971=CARTESIAN_POINT ( 'NONE',  ( 44.99451991528749772, 28.92564299267969474, 4.000000000000000000 ) ) ;
#69972=VERTEX_POINT ( 'NONE', #33657 ) ;
#69974=FACE_OUTER_BOUND ( 'NONE', #122580, .T. ) ;
#69975=DIRECTION ( 'NONE',  ( -0.7071067811865486830, -0.7071067811865464625, -0.000000000000000000 ) ) ;
#69976=CARTESIAN_POINT ( 'NONE',  ( -0.7928932188134458769, 0.7592924766157069794, 5.000000000000000000 ) ) ;
#69977=ORIENTED_EDGE ( 'NONE', *, *, #12056, .T. ) ;
#69979=AXIS2_PLACEMENT_3D ( 'NONE', #34524, #45432, #113488 ) ;
#69980=LINE ( 'NONE', #14103, #63002 ) ;
#69981=AXIS2_PLACEMENT_3D ( 'NONE', #71409, #84444, #116328 ) ;
#69984=AXIS2_PLACEMENT_3D ( 'NONE', #5634, #125310, #27392 ) ;
#69985=CARTESIAN_POINT ( 'NONE',  ( 0.000000000000000000, 0.000000000000000000, 5.000000000000000000 ) ) ;
#69987=ORIENTED_EDGE ( 'NONE', *, *, #106333, .F. ) ;
#69988=AXIS2_PLACEMENT_3D ( 'NONE', #45886, #166, #44463 ) ;
#69989=LINE ( 'NONE', #114152, #45354 ) ;
#69991=DIRECTION ( 'NONE',  ( 0.7071067811865487940, 0.7071067811865463515, 0.000000000000000000 ) ) ;
#69992=DIRECTION ( 'NONE',  ( -0.7071067811865486830, 0.7071067811865464625, 0.000000000000000000 ) ) ;
#69993=CARTESIAN_POINT ( 'NONE',  ( 14.34328999833778262, 3.759292476615678336, 13.27625715073268964 ) ) ;
#69995=CARTESIAN_POINT ( 'NONE',  ( -23.81601139373100295, 28.73617430169770870, 5.000000000000000000 ) ) ;
#69996=LINE ( 'NONE', #6072, #124165 ) ;
#69997=CARTESIAN_POINT ( 'NONE',  ( 31.37176554955596686, -8.240707523384189770, 11.38925528200745596 ) ) ;
#69998=AXIS2_PLACEMENT_3D ( 'NONE', #55945, #89266, #26155 ) ;
#69999=PLANE ( 'NONE',  #69308 ) ;
#70000=EDGE_LOOP ( 'NONE', ( #28335, #115726, #28431, #130126 ) ) ;
#70001=VERTEX_POINT ( 'NONE', #110447 ) ;
#70002=DIRECTION ( 'NONE',  ( -0.3543493200069162685, -0.000000000000000000, -0.9351131265310288487 ) ) ;
#70003=DIRECTION ( 'NONE',  ( 0.7071067811865487940, 0.7071067811865463515, 0.000000000000000000 ) ) ;
#70005=AXIS2_PLACEMENT_3D ( 'NONE', #32523, #131118, #33273 ) ;
#70007=DIRECTION ( 'NONE',  ( 0.7071067811865487940, 0.7071067811865463515, -0.000000000000000000 ) ) ;
#70010=VECTOR ( 'NONE', #88464, 1000.000000000000000 ) ;
#70011=LINE ( 'NONE', #14858, #123284 ) ;
#70013=CARTESIAN_POINT ( 'NONE',  ( -21.51665438641028771, 22.22500000000000142, 4.500000000000000888 ) ) ;
#70014=EDGE_LOOP ( 'NONE', ( #63801, #688, #92448, #64410 ) ) ;
#70016=CARTESIAN_POINT ( 'NONE',  ( -50.99451991528749062, 28.92564299267973738, 4.000000000000000000 ) ) ;
#70018=VERTEX_POINT ( 'NONE', #70419 ) ;
#70019=EDGE_CURVE ( 'NONE', #58035, #34745, #22710, .T. ) ;
#70020=FACE_BOUND ( 'NONE', #15649, .T. ) ;
#70021=CARTESIAN_POINT ( 'NONE',  ( -6.707013264292997157, -21.74070752338405654, 4.999753212805220670 ) ) ;
#70022=DIRECTION ( 'NONE',  ( 0.000000000000000000, 0.000000000000000000, -1.000000000000000000 ) ) ;
#70023=EDGE_CURVE ( 'NONE', #26531, #133481, #45262, .T. ) ;
#70024=CARTESIAN_POINT ( 'NONE',  ( -10.49999999999993250, 13.08746187583912146, 4.000000000000000000 ) ) ;
#70025=VECTOR ( 'NONE', #111449, 1000.000000000000000 ) ;
#70026=DIRECTION ( 'NONE',  ( -0.000000000000000000, -0.000000000000000000, 1.000000000000000000 ) ) ;
#70032=EDGE_LOOP ( 'NONE', ( #16259, #77045, #35717, #58164 ) ) ;
#70033=VERTEX_POINT ( 'NONE', #29690 ) ;
#70035=ORIENTED_EDGE ( 'NONE', *, *, #110551, .F. ) ;
#70036=EDGE_CURVE ( 'NONE', #5681, #63125, #50754, .T. ) ;
#70037=DIRECTION ( 'NONE',  ( 0.6830127018922181881, 0.6830127018922202975, -0.2588190451025214056 ) ) ;
#70038=CARTESIAN_POINT ( 'NONE',  ( -15.15612307739229436, -22.22499999999999432, 4.000000000000000000 ) ) ;
#70039=AXIS2_PLACEMENT_3D ( 'NONE', #11733, #56747, #128 ) ;
#70040=VECTOR ( 'NONE', #133349, 1000.000000000000000 ) ;
#70041=VECTOR ( 'NONE', #17358, 1000.000000000000227 ) ;
#70042=CARTESIAN_POINT ( 'NONE',  ( 7.499999999999954703, 13.46639925780213076, 5.000000000000000000 ) ) ;
#70043=VECTOR ( 'NONE', #97473, 1000.000000000000000 ) ;
#70044=EDGE_CURVE ( 'NONE', #59056, #83800, #126858, .T. ) ;
#70046=LINE ( 'NONE', #114207, #93438 ) ;
#70047=ORIENTED_EDGE ( 'NONE', *, *, #103142, .T. ) ;
#70048=DIRECTION ( 'NONE',  ( -0.000000000000000000, 0.3543493200069153248, 0.9351131265310292928 ) ) ;
#70050=LINE ( 'NONE', #36645, #99050 ) ;
#70051=LINE ( 'NONE', #114892, #122101 ) ;
#70052=CARTESIAN_POINT ( 'NONE',  ( -22.49999999999984723, 22.22500000000000853, 4.362957392718837646 ) ) ;
#70053=VECTOR ( 'NONE', #80660, 1000.000000000000000 ) ;
#70054=VECTOR ( 'NONE', #8188, 1000.000000000000227 ) ;
#70055=VECTOR ( 'NONE', #130064, 1000.000000000000000 ) ;
#70058=ORIENTED_EDGE ( 'NONE', *, *, #115987, .T. ) ;
#70059=CARTESIAN_POINT ( 'NONE',  ( -21.48921356237309155, -27.52281430457070499, 5.000000000000000000 ) ) ;
#70060=PLANE ( 'NONE',  #11818 ) ;
#70061=ORIENTED_EDGE ( 'NONE', *, *, #53978, .T. ) ;
#70062=ORIENTED_EDGE ( 'NONE', *, *, #48911, .T. ) ;
#70063=EDGE_LOOP ( 'NONE', ( #73582, #50616, #1034, #50949 ) ) ;
#70065=ADVANCED_FACE ( 'NONE', ( #93545 ), #115241, .T. ) ;
#70066=ORIENTED_EDGE ( 'NONE', *, *, #98353, .F. ) ;
#70069=ORIENTED_EDGE ( 'NONE', *, *, #96785, .T. ) ;
#70070=CARTESIAN_POINT ( 'NONE',  ( -18.18398860626898994, 28.73617430169800002, 5.000000000000000000 ) ) ;
#70071=EDGE_CURVE ( 'NONE', #73688, #34146, #60816, .T. ) ;
#70072=ORIENTED_EDGE ( 'NONE', *, *, #128752, .F. ) ;
#70073=CARTESIAN_POINT ( 'NONE',  ( 17.48334561358943162, 22.22500000000000142, 4.500000000000000888 ) ) ;
#70074=LINE ( 'NONE', #58498, #123565 ) ;
#70075=VERTEX_POINT ( 'NONE', #15928 ) ;
#70076=ORIENTED_EDGE ( 'NONE', *, *, #91531, .T. ) ;
#70078=VECTOR ( 'NONE', #92823, 1000.000000000000000 ) ;
#70079=DIRECTION ( 'NONE',  ( -0.3543493200069162685, -0.000000000000000000, -0.9351131265310288487 ) ) ;
#70080=EDGE_CURVE ( 'NONE', #27313, #16517, #116721, .T. ) ;
#70081=CARTESIAN_POINT ( 'NONE',  ( 12.99507522778798396, -5.240707523384221744, 12.38332538355493107 ) ) ;
#70082=EDGE_CURVE ( 'NONE', #73359, #57637, #60967, .T. ) ;
#70083=ORIENTED_EDGE ( 'NONE', *, *, #100451, .T. ) ;
#70084=CARTESIAN_POINT ( 'NONE',  ( -27.48921356237309155, -27.52281430457074762, 5.000000000000000000 ) ) ;
#70085=ORIENTED_EDGE ( 'NONE', *, *, #110429, .T. ) ;
#70086=VECTOR ( 'NONE', #52722, 1000.000000000000000 ) ;
#70088=EDGE_LOOP ( 'NONE', ( #19479, #36563, #57294, #71797 ) ) ;
#70091=AXIS2_PLACEMENT_3D ( 'NONE', #37690, #16612, #71744 ) ;
#70092=EDGE_CURVE ( 'NONE', #82948, #140430, #18075, .T. ) ;
#70093=CARTESIAN_POINT ( 'NONE',  ( 27.18398860626900060, 28.73617430169806042, 5.000000000000000000 ) ) ;
#70094=CARTESIAN_POINT ( 'NONE',  ( -8.671830600776413434, -9.740707523384187994, 4.000000000000000000 ) ) ;
#70095=EDGE_CURVE ( 'NONE', #6993, #83571, #60218, .T. ) ;
#70097=LINE ( 'NONE', #14932, #134572 ) ;
#70098=ORIENTED_EDGE ( 'NONE', *, *, #26235, .T. ) ;
#70099=DIRECTION ( 'NONE',  ( 1.000000000000000000, 0.000000000000000000, 0.000000000000000000 ) ) ;
#70102=DIRECTION ( 'NONE',  ( 0.7071067811865487940, 0.7071067811865463515, 0.000000000000000000 ) ) ;
#70103=( BOUNDED_CURVE ( )  B_SPLINE_CURVE ( 3, ( #139189, #104373, #5034, #82649 ),
 .UNSPECIFIED., .F., .T. ) 
 B_SPLINE_CURVE_WITH_KNOTS ( ( 4, 4 ),
 ( 4.987589563512864643, 5.034563671340741564 ),
 .UNSPECIFIED. ) 
 CURVE ( )  GEOMETRIC_REPRESENTATION_ITEM ( )  RATIONAL_B_SPLINE_CURVE ( ( 1.000000000000000000, 0.9998161278856747547, 0.9998161278856747547, 1.000000000000000000 ) ) 
 REPRESENTATION_ITEM ( '' )  );
#70104=ADVANCED_FACE ( 'NONE', ( #106521 ), #6474, .F. ) ;
#70107=EDGE_LOOP ( 'NONE', ( #51108, #29303, #56660, #140382, #60560, #112102 ) ) ;
#70108=VECTOR ( 'NONE', #70714, 1000.000000000000000 ) ;
#70109=ORIENTED_EDGE ( 'NONE', *, *, #131011, .F. ) ;
#70110=CARTESIAN_POINT ( 'NONE',  ( 57.29974487139158157, -27.71228299555246011, 4.000000000000000000 ) ) ;
#70111=DIRECTION ( 'NONE',  ( 0.6830127018922180770, -0.6830127018922204085, -0.2588190451025213501 ) ) ;
#70112=PLANE ( 'NONE',  #94001 ) ;
#70113=AXIS2_PLACEMENT_3D ( 'NONE', #54788, #55500, #77962 ) ;
#70114=LINE ( 'NONE', #36706, #107583 ) ;
#70116=DIRECTION ( 'NONE',  ( -0.6830127018922180770, -0.6830127018922204085, -0.2588190451025213501 ) ) ;
#70118=DIRECTION ( 'NONE',  ( -0.000000000000000000, 0.000000000000000000, 1.000000000000000000 ) ) ;
#70119=DIRECTION ( 'NONE',  ( 0.3543493200069162685, -0.000000000000000000, -0.9351131265310288487 ) ) ;
#70120=LINE ( 'NONE', #39607, #51847 ) ;
#70121=DIRECTION ( 'NONE',  ( -0.7071067811865486830, -0.7071067811865464625, 0.000000000000000000 ) ) ;
#70122=DIRECTION ( 'NONE',  ( -0.7071067811865486830, 0.7071067811865464625, 0.000000000000000000 ) ) ;
#70124=VECTOR ( 'NONE', #83164, 1000.000000000000000 ) ;
#70126=ORIENTED_EDGE ( 'NONE', *, *, #69537, .T. ) ;
#70127=CARTESIAN_POINT ( 'NONE',  ( 8.999999999999937828, 16.93112307739201583, 4.000000000000000000 ) ) ;
#70128=DIRECTION ( 'NONE',  ( -0.3543493200069163240, -0.000000000000000000, 0.9351131265310288487 ) ) ;
#70130=PLANE ( 'NONE',  #125039 ) ;
#70131=CARTESIAN_POINT ( 'NONE',  ( -2.510786437626908008, -27.52281430457053446, 5.000000000000000000 ) ) ;
#70132=EDGE_LOOP ( 'NONE', ( #117367, #52107, #101951, #24599 ) ) ;
#70134=AXIS2_PLACEMENT_3D ( 'NONE', #122516, #110909, #65708 ) ;
#70135=ORIENTED_EDGE ( 'NONE', *, *, #93063, .T. ) ;
#70137=ORIENTED_EDGE ( 'NONE', *, *, #15132, .F. ) ;
#70140=FACE_OUTER_BOUND ( 'NONE', #12383, .T. ) ;
#70141=CARTESIAN_POINT ( 'NONE',  ( 38.99451991528749062, 28.92564299267965211, 4.000000000000000000 ) ) ;
#70142=ORIENTED_EDGE ( 'NONE', *, *, #77776, .F. ) ;
#70143=LINE ( 'NONE', #58563, #107095 ) ;
#70144=DIRECTION ( 'NONE',  ( -0.7071067811865486830, -0.7071067811865464625, -0.000000000000000000 ) ) ;
#70145=CARTESIAN_POINT ( 'NONE',  ( 36.29974487139159578, -27.71228299555231445, 4.000000000000000000 ) ) ;
#70147=FACE_OUTER_BOUND ( 'NONE', #63106, .T. ) ;
#70148=VECTOR ( 'NONE', #37810, 1000.000000000000000 ) ;
#70149=AXIS2_PLACEMENT_3D ( 'NONE', #951, #21306, #99548 ) ;
#70150=LINE ( 'NONE', #46237, #72161 ) ;
#70151=PLANE ( 'NONE',  #133493 ) ;
#70152=ORIENTED_EDGE ( 'NONE', *, *, #72843, .F. ) ;
#70153=VECTOR ( 'NONE', #4529, 999.9999999999998863 ) ;
#70154=VECTOR ( 'NONE', #21335, 1000.000000000000227 ) ;
#70155=FACE_OUTER_BOUND ( 'NONE', #123309, .T. ) ;
#70156=ORIENTED_EDGE ( 'NONE', *, *, #80356, .F. ) ;
#70158=FACE_OUTER_BOUND ( 'NONE', #56100, .T. ) ;
#70159=CARTESIAN_POINT ( 'NONE',  ( -20.99451991528748707, 28.92564299267952777, 4.000000000000000000 ) ) ;
#70161=DIRECTION ( 'NONE',  ( 0.7071067811865487940, 0.7071067811865463515, 0.000000000000000000 ) ) ;
#70162=VECTOR ( 'NONE', #140021, 1000.000000000000227 ) ;
#70163=DIRECTION ( 'NONE',  ( -0.3543493200069162685, -0.000000000000000000, -0.9351131265310288487 ) ) ;
#70164=ORIENTED_EDGE ( 'NONE', *, *, #42871, .T. ) ;
#70168=DIRECTION ( 'NONE',  ( -0.7071067811865487940, 0.7071067811865463515, 0.000000000000000000 ) ) ;
#70171=ORIENTED_EDGE ( 'NONE', *, *, #8104, .T. ) ;
#70172=FACE_OUTER_BOUND ( 'NONE', #55932, .T. ) ;
#70173=PLANE ( 'NONE',  #93932 ) ;
#70174=PLANE ( 'NONE',  #114162 ) ;
#70175=DIRECTION ( 'NONE',  ( 0.6830127018922181881, 0.6830127018922202975, -0.2588190451025214056 ) ) ;
#70176=VERTEX_POINT ( 'NONE', #53620 ) ;
#70177=ORIENTED_EDGE ( 'NONE', *, *, #71068, .T. ) ;
#70180=AXIS2_PLACEMENT_3D ( 'NONE', #6898, #9026, #32278 ) ;
#70181=EDGE_LOOP ( 'NONE', ( #141625, #93084, #64569, #79490, #46431, #17492 ) ) ;
#70182=LINE ( 'NONE', #92570, #63730 ) ;
#70183=CARTESIAN_POINT ( 'NONE',  ( -23.96628934044694148, -0.2106608083017154909, 4.443784815937080523 ) ) ;
#70184=EDGE_CURVE ( 'NONE', #107596, #63680, #31160, .T. ) ;
#70185=DIRECTION ( 'NONE',  ( -0.3543493200069162685, -0.000000000000000000, -0.9351131265310288487 ) ) ;
#70186=DIRECTION ( 'NONE',  ( -0.7071067811865486830, -0.7071067811865464625, 0.000000000000000000 ) ) ;
#70187=ORIENTED_EDGE ( 'NONE', *, *, #55010, .F. ) ;
#70189=PLANE ( 'NONE',  #83706 ) ;
#70190=AXIS2_PLACEMENT_3D ( 'NONE', #33851, #11320, #88948 ) ;
#70192=ADVANCED_FACE ( 'NONE', ( #132633 ), #21693, .F. ) ;
#70193=ORIENTED_EDGE ( 'NONE', *, *, #80977, .F. ) ;
#70194=VECTOR ( 'NONE', #136541, 1000.000000000000000 ) ;
#70195=CARTESIAN_POINT ( 'NONE',  ( -24.29974487139158867, -27.71228299555223273, 4.000000000000000000 ) ) ;
#70199=ORIENTED_EDGE ( 'NONE', *, *, #2211, .F. ) ;
#70200=ORIENTED_EDGE ( 'NONE', *, *, #52155, .T. ) ;
#70201=EDGE_CURVE ( 'NONE', #34867, #67596, #69149, .T. ) ;
#70203=EDGE_CURVE ( 'NONE', #35082, #110223, #34366, .T. ) ;
#70204=EDGE_CURVE ( 'NONE', #34556, #82308, #132993, .T. ) ;
#70205=CARTESIAN_POINT ( 'NONE',  ( -33.32816939922329880, 14.25929247661557397, 4.000000000000000000 ) ) ;
#70206=FACE_OUTER_BOUND ( 'NONE', #94574, .T. ) ;
#70207=DIRECTION ( 'NONE',  ( 0.7071067811865487940, 0.7071067811865463515, 0.000000000000000000 ) ) ;
#70209=LINE ( 'NONE', #57175, #58075 ) ;
#70211=ADVANCED_FACE ( 'NONE', ( #123543 ), #143118, .T. ) ;
#70212=EDGE_CURVE ( 'NONE', #56310, #45046, #1683, .T. ) ;
#70213=CARTESIAN_POINT ( 'NONE',  ( 47.99451991528749062, 28.92564299267971251, 4.000000000000000000 ) ) ;
#70214=EDGE_LOOP ( 'NONE', ( #125300, #52163, #141924, #127354, #102470 ) ) ;
#70215=VERTEX_POINT ( 'NONE', #121355 ) ;
#70216=DIRECTION ( 'NONE',  ( 0.7071067811865487940, -0.7071067811865463515, 0.000000000000000000 ) ) ;
#70217=ADVANCED_FACE ( 'NONE', ( #22038 ), #66291, .F. ) ;
#70218=EDGE_LOOP ( 'NONE', ( #91572, #100424, #80373, #123279 ) ) ;
#70219=AXIS2_PLACEMENT_3D ( 'NONE', #69294, #67900, #122952 ) ;
#70220=VECTOR ( 'NONE', #38033, 1000.000000000000227 ) ;
#70221=ADVANCED_FACE ( 'NONE', ( #72023 ), #70602, .F. ) ;
#70223=ORIENTED_EDGE ( 'NONE', *, *, #46794, .T. ) ;
#70224=DIRECTION ( 'NONE',  ( 0.6830127018922181881, 0.6830127018922202975, -0.2588190451025214056 ) ) ;
#70225=DIRECTION ( 'NONE',  ( -0.7071067811865486830, -0.7071067811865464625, 0.000000000000000000 ) ) ;
#70226=CARTESIAN_POINT ( 'NONE',  ( 0.000000000000000000, 0.000000000000000000, 5.000000000000000000 ) ) ;
#70227=VECTOR ( 'NONE', #36007, 999.9999999999998863 ) ;
#70229=ORIENTED_EDGE ( 'NONE', *, *, #11055, .F. ) ;
#70230=DIRECTION ( 'NONE',  ( 0.000000000000000000, -1.000000000000000000, 0.000000000000000000 ) ) ;
#70231=ORIENTED_EDGE ( 'NONE', *, *, #101551, .T. ) ;
#70232=CARTESIAN_POINT ( 'NONE',  ( -17.51078643762690845, -27.52281430457043143, 5.000000000000000000 ) ) ;
#70233=EDGE_LOOP ( 'NONE', ( #99446, #38056, #57638, #4487 ) ) ;
#70235=PLANE ( 'NONE',  #76037 ) ;
#70237=ORIENTED_EDGE ( 'NONE', *, *, #30062, .T. ) ;
#70238=AXIS2_PLACEMENT_3D ( 'NONE', #15689, #107020, #72315 ) ;
#70239=LINE ( 'NONE', #32760, #97395 ) ;
#70241=EDGE_LOOP ( 'NONE', ( #84375, #131574, #94799, #132026 ) ) ;
#70242=DIRECTION ( 'NONE',  ( 0.7071067811865486830, -0.7071067811865464625, -0.000000000000000000 ) ) ;
#70243=CARTESIAN_POINT ( 'NONE',  ( 9.183988606268997046, 28.73617430169793607, 5.000000000000000000 ) ) ;
#70246=DIRECTION ( 'NONE',  ( -0.6830127018922180770, -0.6830127018922204085, -0.2588190451025213501 ) ) ;
#70247=EDGE_CURVE ( 'NONE', #64709, #109374, #102494, .T. ) ;
#70248=LINE ( 'NONE', #114408, #23215 ) ;
#70250=CARTESIAN_POINT ( 'NONE',  ( 1.828169399223505964, 21.75929247661551358, 4.000000000000000000 ) ) ;
#70253=ADVANCED_FACE ( 'NONE', ( #71291 ), #39377, .F. ) ;
#70254=ORIENTED_EDGE ( 'NONE', *, *, #91372, .F. ) ;
#70255=CARTESIAN_POINT ( 'NONE',  ( -7.499999999999944045, -7.533600742197667621, 5.000000000000000000 ) ) ;
#70257=EDGE_LOOP ( 'NONE', ( #106948, #43066, #18254, #108327 ) ) ;
#70258=EDGE_CURVE ( 'NONE', #132991, #129216, #59023, .T. ) ;
#70259=VERTEX_POINT ( 'NONE', #17581 ) ;
#70260=VECTOR ( 'NONE', #3763, 1000.000000000000000 ) ;
#70262=CARTESIAN_POINT ( 'NONE',  ( 1.499999999999980460, 19.08746187583906462, 4.000000000000000000 ) ) ;
#70263=ORIENTED_EDGE ( 'NONE', *, *, #7157, .F. ) ;
#70265=EDGE_CURVE ( 'NONE', #72157, #104640, #48105, .T. ) ;
#70266=DIRECTION ( 'NONE',  ( -0.7071067811865486830, -0.7071067811865464625, -0.000000000000000000 ) ) ;
#70267=CARTESIAN_POINT ( 'NONE',  ( 34.49999999999976552, -7.420205493532866292, -2.617629953481174887 ) ) ;
#70268=CARTESIAN_POINT ( 'NONE',  ( 25.17183060077628909, 18.75929247661551713, 4.000000000000000000 ) ) ;
#70269=CARTESIAN_POINT ( 'NONE',  ( 27.70710678118635428, 14.25929247661557397, 5.000000000000000000 ) ) ;
#70270=VERTEX_POINT ( 'NONE', #49555 ) ;
#70272=ORIENTED_EDGE ( 'NONE', *, *, #29604, .T. ) ;
#70273=EDGE_CURVE ( 'NONE', #115863, #83494, #127813, .T. ) ;
#70274=DIRECTION ( 'NONE',  ( -0.000000000000000000, 0.000000000000000000, 1.000000000000000000 ) ) ;
#70277=LINE ( 'NONE', #48466, #29740 ) ;
#70278=EDGE_CURVE ( 'NONE', #37747, #48700, #15420, .T. ) ;
#70279=DIRECTION ( 'NONE',  ( -0.6830127018922181881, 0.6830127018922202975, -0.2588190451025214056 ) ) ;
#70280=VERTEX_POINT ( 'NONE', #37214 ) ;
#70281=VERTEX_POINT ( 'NONE', #137969 ) ;
#70282=ORIENTED_EDGE ( 'NONE', *, *, #136210, .T. ) ;
#70283=CARTESIAN_POINT ( 'NONE',  ( 5.292893218813419232, 17.25929247661554911, 5.000000000000000000 ) ) ;
#70285=CARTESIAN_POINT ( 'NONE',  ( 11.20710678118646442, 18.75929247661552068, 5.000000000000000000 ) ) ;
#70286=DIRECTION ( 'NONE',  ( -0.7071067811865486830, 0.7071067811865464625, 0.000000000000000000 ) ) ;
#70287=ORIENTED_EDGE ( 'NONE', *, *, #52332, .F. ) ;
#70288=VECTOR ( 'NONE', #10625, 1000.000000000000000 ) ;
#70289=LINE ( 'NONE', #5660, #118000 ) ;
#70290=CARTESIAN_POINT ( 'NONE',  ( 30.29974487139158867, -27.71228299555227537, 4.000000000000000000 ) ) ;
#70291=AXIS2_PLACEMENT_3D ( 'NONE', #47217, #52553, #142442 ) ;
#70292=DIRECTION ( 'NONE',  ( 0.7071067811865487940, 0.7071067811865463515, -0.000000000000000000 ) ) ;
#70293=CARTESIAN_POINT ( 'NONE',  ( 75.29974487139158157, -27.71228299555258445, 4.000000000000000000 ) ) ;
#70294=ORIENTED_EDGE ( 'NONE', *, *, #131370, .T. ) ;
#70296=ORIENTED_EDGE ( 'NONE', *, *, #95678, .F. ) ;
#70297=AXIS2_PLACEMENT_3D ( 'NONE', #82363, #126545, #38144 ) ;
#70298=DIRECTION ( 'NONE',  ( -0.6830127018922180770, -0.6830127018922204085, -0.2588190451025213501 ) ) ;
#70299=ORIENTED_EDGE ( 'NONE', *, *, #69670, .T. ) ;
#70300=EDGE_CURVE ( 'NONE', #42962, #92514, #104607, .T. ) ;
#70301=VERTEX_POINT ( 'NONE', #61166 ) ;
#70303=DIRECTION ( 'NONE',  ( 0.6830127018922180770, -0.6830127018922204085, -0.2588190451025213501 ) ) ;
#70305=DIRECTION ( 'NONE',  ( -0.7071067811865486830, -0.7071067811865464625, 0.000000000000000000 ) ) ;
#70306=VERTEX_POINT ( 'NONE', #80742 ) ;
#70308=LINE ( 'NONE', #59415, #19715 ) ;
#70311=LINE ( 'NONE', #36904, #71696 ) ;
#70312=VECTOR ( 'NONE', #97493, 1000.000000000000000 ) ;
#70315=DIRECTION ( 'NONE',  ( -0.000000000000000000, 0.000000000000000000, 1.000000000000000000 ) ) ;
#70316=DIRECTION ( 'NONE',  ( 1.000000000000000000, 0.000000000000000000, 0.000000000000000000 ) ) ;
#70319=VECTOR ( 'NONE', #3404, 1000.000000000000000 ) ;
#70320=LINE ( 'NONE', #114468, #43662 ) ;
#70321=CARTESIAN_POINT ( 'NONE',  ( -32.99999999999976552, -18.41253812416056945, 4.000000000000000000 ) ) ;
#70322=CARTESIAN_POINT ( 'NONE',  ( 21.48921356237309155, -27.52281430457070499, 5.000000000000000000 ) ) ;
#70323=VERTEX_POINT ( 'NONE', #124931 ) ;
#70324=EDGE_CURVE ( 'NONE', #122875, #116985, #125667, .T. ) ;
#70327=EDGE_CURVE ( 'NONE', #34745, #54071, #141089, .T. ) ;
#70328=ORIENTED_EDGE ( 'NONE', *, *, #90345, .T. ) ;
#70329=VERTEX_POINT ( 'NONE', #25612 ) ;
#70330=CARTESIAN_POINT ( 'NONE',  ( 21.48921356237309155, -27.52281430457070499, 5.000000000000000000 ) ) ;
#70331=CARTESIAN_POINT ( 'NONE',  ( 20.99999999999985434, -13.06887692260767686, 4.000000000000000000 ) ) ;
#70332=AXIS2_PLACEMENT_3D ( 'NONE', #43137, #141738, #131563 ) ;
#70334=ORIENTED_EDGE ( 'NONE', *, *, #30710, .T. ) ;
#70336=CARTESIAN_POINT ( 'NONE',  ( 66.48921356237309510, -27.52281430457101763, 5.000000000000000000 ) ) ;
#70337=DIRECTION ( 'NONE',  ( -0.7071067811865486830, 0.7071067811865464625, 0.000000000000000000 ) ) ;
#70338=FACE_OUTER_BOUND ( 'NONE', #15921, .T. ) ;
#70340=LINE ( 'NONE', #82593, #19251 ) ;
#70341=CARTESIAN_POINT ( 'NONE',  ( 28.49999999999980460, 3.052185695429140200, 5.000000000000000000 ) ) ;
#70342=VECTOR ( 'NONE', #1097, 1000.000000000000227 ) ;
#70343=FACE_OUTER_BOUND ( 'NONE', #119659, .T. ) ;
#70344=DIRECTION ( 'NONE',  ( 0.6830127018922181881, 0.6830127018922202975, -0.2588190451025214056 ) ) ;
#70345=LINE ( 'NONE', #25349, #109403 ) ;
#70347=DIRECTION ( 'NONE',  ( -0.000000000000000000, 0.000000000000000000, 1.000000000000000000 ) ) ;
#70349=ORIENTED_EDGE ( 'NONE', *, *, #113858, .T. ) ;
#70350=ORIENTED_EDGE ( 'NONE', *, *, #59603, .T. ) ;
#70352=AXIS2_PLACEMENT_3D ( 'NONE', #115080, #17909, #73759 ) ;
#70353=ORIENTED_EDGE ( 'NONE', *, *, #19468, .T. ) ;
#70354=DIRECTION ( 'NONE',  ( 0.000000000000000000, -1.000000000000000000, 0.000000000000000000 ) ) ;
#70355=CARTESIAN_POINT ( 'NONE',  ( 6.938893903907228378E-15, 5.966399257802203593, 5.000000000000000000 ) ) ;
#70356=EDGE_LOOP ( 'NONE', ( #65803, #29241, #87032 ) ) ;
#70357=DIRECTION ( 'NONE',  ( -0.6830127018922180770, 0.6830127018922202975, -0.2588190451025213501 ) ) ;
#70358=CARTESIAN_POINT ( 'NONE',  ( -39.18398860626899705, 28.73617430169814568, 5.000000000000000000 ) ) ;
#70359=AXIS2_PLACEMENT_3D ( 'NONE', #109216, #109928, #117913 ) ;
#70362=ORIENTED_EDGE ( 'NONE', *, *, #69759, .F. ) ;
#70363=DIRECTION ( 'NONE',  ( 0.6830127018922181881, 0.6830127018922202975, -0.2588190451025214056 ) ) ;
#70364=CARTESIAN_POINT ( 'NONE',  ( 30.09667064187387098, -2.240707523384257716, 15.26439735382759544 ) ) ;
#70365=CARTESIAN_POINT ( 'NONE',  ( -12.48921356237309155, -27.52281430457064104, 5.000000000000000000 ) ) ;
#70366=FACE_OUTER_BOUND ( 'NONE', #85917, .T. ) ;
#70369=ORIENTED_EDGE ( 'NONE', *, *, #123082, .T. ) ;
#70371=ADVANCED_FACE ( 'NONE', ( #127068 ), #27757, .F. ) ;
#70374=ADVANCED_FACE ( 'NONE', ( #140786 ), #87145, .F. ) ;
#70375=EDGE_CURVE ( 'NONE', #66060, #91002, #29887, .T. ) ;
#70377=VECTOR ( 'NONE', #107855, 1000.000000000000000 ) ;
#70379=EDGE_CURVE ( 'NONE', #15864, #76116, #29186, .T. ) ;
#70381=EDGE_LOOP ( 'NONE', ( #117167, #83379, #120549, #102167 ) ) ;
#70383=EDGE_CURVE ( 'NONE', #45317, #100766, #95867, .T. ) ;
#70384=VERTEX_POINT ( 'NONE', #141531 ) ;
#70387=VECTOR ( 'NONE', #137981, 1000.000000000000000 ) ;
#70388=DIRECTION ( 'NONE',  ( 0.7071067811865487940, 0.7071067811865463515, 0.000000000000000000 ) ) ;
#70389=EDGE_CURVE ( 'NONE', #19080, #14379, #40794, .T. ) ;
#70390=CARTESIAN_POINT ( 'NONE',  ( -38.01844734635646006, 18.75929247661552424, 20.33588619593452052 ) ) ;
#70393=CARTESIAN_POINT ( 'NONE',  ( 78.29974487139158157, -27.71228299555260577, 4.000000000000000000 ) ) ;
#70394=PLANE ( 'NONE',  #83064 ) ;
#70396=LINE ( 'NONE', #114548, #2643 ) ;
#70397=VECTOR ( 'NONE', #64713, 1000.000000000000000 ) ;
#70398=ADVANCED_FACE ( 'NONE', ( #18278 ), #63972, .T. ) ;
#70399=CARTESIAN_POINT ( 'NONE',  ( 7.499999999999947597, 18.43112307739200162, 4.000000000000000000 ) ) ;
#70400=FACE_BOUND ( 'NONE', #31024, .T. ) ;
#70401=VECTOR ( 'NONE', #123382, 1000.000000000000000 ) ;
#70402=VERTEX_POINT ( 'NONE', #139419 ) ;
#70403=EDGE_CURVE ( 'NONE', #4116, #114666, #31344, .T. ) ;
#70404=LINE ( 'NONE', #5772, #66602 ) ;
#70405=PLANE ( 'NONE',  #106298 ) ;
#70406=DIRECTION ( 'NONE',  ( -0.6830127018922181881, 0.6830127018922202975, -0.2588190451025214056 ) ) ;
#70409=VERTEX_POINT ( 'NONE', #118324 ) ;
#70410=EDGE_LOOP ( 'NONE', ( #68818, #16665, #76833, #14233 ) ) ;
#70412=EDGE_CURVE ( 'NONE', #112632, #136524, #86446, .T. ) ;
#70414=AXIS2_PLACEMENT_3D ( 'NONE', #76817, #110804, #99967 ) ;
#70417=ORIENTED_EDGE ( 'NONE', *, *, #73173, .T. ) ;
#70418=CARTESIAN_POINT ( 'NONE',  ( 9.183988606268997046, 28.73617430169793607, 5.000000000000000000 ) ) ;
#70419=CARTESIAN_POINT ( 'NONE',  ( -34.92500000000001137, 13.51246187583936198, 4.000000000000000000 ) ) ;
#70421=EDGE_LOOP ( 'NONE', ( #68075, #70076, #51664, #125683 ) ) ;
#70422=CARTESIAN_POINT ( 'NONE',  ( 48.29974487139158867, -27.71228299555239971, 4.000000000000000000 ) ) ;
#70424=DIRECTION ( 'NONE',  ( 0.6830127018922180770, -0.6830127018922204085, -0.2588190451025213501 ) ) ;
#70425=DIRECTION ( 'NONE',  ( -0.7071067811865487940, 0.7071067811865463515, -0.000000000000000000 ) ) ;
#70426=DIRECTION ( 'NONE',  ( 1.000000000000000000, 0.000000000000000000, 0.000000000000000000 ) ) ;
#70427=CARTESIAN_POINT ( 'NONE',  ( -45.18398860626900415, 28.73617430169818832, 5.000000000000000000 ) ) ;
#70429=EDGE_CURVE ( 'NONE', #32288, #48528, #8121, .T. ) ;
#70430=ORIENTED_EDGE ( 'NONE', *, *, #50144, .F. ) ;
#70433=ORIENTED_EDGE ( 'NONE', *, *, #65135, .T. ) ;
#70436=ORIENTED_EDGE ( 'NONE', *, *, #132035, .F. ) ;
#70437=LINE ( 'NONE', #58853, #93012 ) ;
#70438=LINE ( 'NONE', #92838, #78713 ) ;
#70439=ORIENTED_EDGE ( 'NONE', *, *, #47757, .T. ) ;
#70441=ORIENTED_EDGE ( 'NONE', *, *, #3500, .T. ) ;
#70442=ADVANCED_FACE ( 'NONE', ( #50957 ), #20434, .F. ) ;
#70443=DIRECTION ( 'NONE',  ( 0.7071067811865486830, -0.7071067811865464625, -0.000000000000000000 ) ) ;
#70444=CARTESIAN_POINT ( 'NONE',  ( -75.29974487139158157, -27.71228299555258445, 4.000000000000000000 ) ) ;
#70445=VECTOR ( 'NONE', #106013, 1000.000000000000000 ) ;
#70446=VERTEX_POINT ( 'NONE', #64683 ) ;
#70449=DIRECTION ( 'NONE',  ( 0.6830127018922180770, -0.6830127018922204085, -0.2588190451025213501 ) ) ;
#70451=CARTESIAN_POINT ( 'NONE',  ( 0.000000000000000000, 0.000000000000000000, 5.000000000000000000 ) ) ;
#70452=ORIENTED_EDGE ( 'NONE', *, *, #24362, .F. ) ;
#70453=ORIENTED_EDGE ( 'NONE', *, *, #69032, .T. ) ;
#70454=DIRECTION ( 'NONE',  ( -0.7071067811865486830, -0.7071067811865464625, -0.000000000000000000 ) ) ;
#70455=ORIENTED_EDGE ( 'NONE', *, *, #117610, .T. ) ;
#70456=CARTESIAN_POINT ( 'NONE',  ( -9.707106781186478628, 8.259292476615632594, 5.000000000000000000 ) ) ;
#70458=DIRECTION ( 'NONE',  ( -0.7071067811865486830, -0.7071067811865464625, 0.000000000000000000 ) ) ;
#70459=DIRECTION ( 'NONE',  ( 0.6830127018922180770, -0.6830127018922204085, -0.2588190451025213501 ) ) ;
#70461=VECTOR ( 'NONE', #18610, 1000.000000000000000 ) ;
#70462=VERTEX_POINT ( 'NONE', #84996 ) ;
#70463=CARTESIAN_POINT ( 'NONE',  ( 75.48921356237309510, -27.52281430457107803, 5.000000000000000000 ) ) ;
#70464=EDGE_CURVE ( 'NONE', #23833, #17476, #92547, .T. ) ;
#70465=DIRECTION ( 'NONE',  ( -0.6830127018922181881, 0.6830127018922202975, -0.2588190451025214056 ) ) ;
#70466=CARTESIAN_POINT ( 'NONE',  ( 19.49999999999987210, 18.43112307739199451, 4.000000000000000000 ) ) ;
#70467=ORIENTED_EDGE ( 'NONE', *, *, #6738, .T. ) ;
#70468=PLANE ( 'NONE',  #120656 ) ;
#70469=DIRECTION ( 'NONE',  ( 0.7071067811865487940, 0.7071067811865463515, 0.000000000000000000 ) ) ;
#70470=ORIENTED_EDGE ( 'NONE', *, *, #13089, .F. ) ;
#70471=DIRECTION ( 'NONE',  ( 0.6830127018922180770, -0.6830127018922204085, -0.2588190451025213501 ) ) ;
#70473=ADVANCED_FACE ( 'NONE', ( #52364 ), #142260, .F. ) ;
#70475=DIRECTION ( 'NONE',  ( 0.7071067811865486830, -0.7071067811865464625, -0.000000000000000000 ) ) ;
#70476=DIRECTION ( 'NONE',  ( 0.7071067811865487940, -0.7071067811865463515, 0.000000000000000000 ) ) ;
#70477=AXIS2_PLACEMENT_3D ( 'NONE', #75893, #123703, #68603 ) ;
#70478=ORIENTED_EDGE ( 'NONE', *, *, #15017, .T. ) ;
#70479=CARTESIAN_POINT ( 'NONE',  ( 20.81601139373100295, 28.73617430169773002, 5.000000000000000000 ) ) ;
#70480=DIRECTION ( 'NONE',  ( -0.7071067811865486830, 0.7071067811865464625, 0.000000000000000000 ) ) ;
#70481=VECTOR ( 'NONE', #113582, 999.9999999999998863 ) ;
#70482=EDGE_CURVE ( 'NONE', #65352, #13630, #19733, .T. ) ;
#70485=VECTOR ( 'NONE', #126587, 1000.000000000000227 ) ;
#70486=DIRECTION ( 'NONE',  ( 0.3543493200069162685, -0.000000000000000000, -0.9351131265310288487 ) ) ;
#70487=DIRECTION ( 'NONE',  ( 0.7071067811865486830, -0.7071067811865464625, -0.000000000000000000 ) ) ;
#70488=LINE ( 'NONE', #57442, #33173 ) ;
#70490=CARTESIAN_POINT ( 'NONE',  ( -34.92500000000001137, -5.240707523384228850, 4.255531930566255561 ) ) ;
#70491=FACE_OUTER_BOUND ( 'NONE', #82495, .T. ) ;
#70493=ADVANCED_FACE ( 'NONE', ( #89977 ), #819, .F. ) ;
#70494=ORIENTED_EDGE ( 'NONE', *, *, #97573, .T. ) ;
#70497=EDGE_CURVE ( 'NONE', #30921, #5268, #34198, .T. ) ;
#70498=VERTEX_POINT ( 'NONE', #134962 ) ;
#70500=VERTEX_POINT ( 'NONE', #66126 ) ;
#70502=VERTEX_POINT ( 'NONE', #100173 ) ;
#70503=LINE ( 'NONE', #114646, #96440 ) ;
#70504=LINE ( 'NONE', #114647, #124983 ) ;
#70505=ORIENTED_EDGE ( 'NONE', *, *, #43535, .T. ) ;
#70506=DIRECTION ( 'NONE',  ( 0.7071067811865487940, 0.7071067811865463515, -0.000000000000000000 ) ) ;
#70507=CARTESIAN_POINT ( 'NONE',  ( 0.4892135623730947680, -27.52281430457055578, 5.000000000000000000 ) ) ;
#70509=LINE ( 'NONE', #15322, #86 ) ;
#70511=ORIENTED_EDGE ( 'NONE', *, *, #93080, .F. ) ;
#70513=CARTESIAN_POINT ( 'NONE',  ( -9.183988606268997046, 28.73617430169793607, 5.000000000000000000 ) ) ;
#70514=LINE ( 'NONE', #114657, #128388 ) ;
#70515=DIRECTION ( 'NONE',  ( -0.7071067811865486830, -0.7071067811865464625, 0.000000000000000000 ) ) ;
#70517=PLANE ( 'NONE',  #79345 ) ;
#70518=DIRECTION ( 'NONE',  ( -0.6830127018922181881, 0.6830127018922202975, -0.2588190451025214056 ) ) ;
#70519=VECTOR ( 'NONE', #84157, 1000.000000000000000 ) ;
#70521=DIRECTION ( 'NONE',  ( -0.7071067811865487940, 0.7071067811865463515, -0.000000000000000000 ) ) ;
#70522=VECTOR ( 'NONE', #104966, 999.9999999999998863 ) ;
#70524=ORIENTED_EDGE ( 'NONE', *, *, #139242, .T. ) ;
#70525=AXIS2_PLACEMENT_3D ( 'NONE', #61696, #105856, #141366 ) ;
#70527=ORIENTED_EDGE ( 'NONE', *, *, #45824, .F. ) ;
#70528=VERTEX_POINT ( 'NONE', #89285 ) ;
#70529=DIRECTION ( 'NONE',  ( 0.6830127018922180770, 0.6830127018922202975, -0.2588190451025213501 ) ) ;
#70530=DIRECTION ( 'NONE',  ( -0.7071067811865487940, 0.7071067811865463515, 0.000000000000000000 ) ) ;
#70531=ORIENTED_EDGE ( 'NONE', *, *, #75296, .F. ) ;
#70532=PLANE ( 'NONE',  #101283 ) ;
#70534=DIRECTION ( 'NONE',  ( -0.7071067811865486830, -0.7071067811865464625, -0.000000000000000000 ) ) ;
#70535=VECTOR ( 'NONE', #119201, 1000.000000000000000 ) ;
#70537=ORIENTED_EDGE ( 'NONE', *, *, #15045, .F. ) ;
#70538=LINE ( 'NONE', #15352, #108095 ) ;
#70539=ORIENTED_EDGE ( 'NONE', *, *, #125007, .T. ) ;
#70540=DIRECTION ( 'NONE',  ( -0.7071067811865486830, -0.7071067811865464625, 0.000000000000000000 ) ) ;
#70541=CARTESIAN_POINT ( 'NONE',  ( 31.49999999999978684, 21.05218569542895679, 5.000000000000000000 ) ) ;
#70543=PLANE ( 'NONE',  #102017 ) ;
#70544=ORIENTED_EDGE ( 'NONE', *, *, #94707, .T. ) ;
#70545=ORIENTED_EDGE ( 'NONE', *, *, #23372, .F. ) ;
#70546=CARTESIAN_POINT ( 'NONE',  ( 31.49999999999977973, -6.839392718269103888, -8.480912228396157104 ) ) ;
#70547=PLANE ( 'NONE',  #73988 ) ;
#70548=CARTESIAN_POINT ( 'NONE',  ( -42.29974487139158157, -27.71228299555235708, 4.000000000000000000 ) ) ;
#70549=EDGE_CURVE ( 'NONE', #47748, #68933, #23283, .T. ) ;
#70551=ADVANCED_FACE ( 'NONE', ( #88591 ), #90733, .T. ) ;
#70554=EDGE_CURVE ( 'NONE', #63130, #86567, #45803, .T. ) ;
#70557=DIRECTION ( 'NONE',  ( 0.7071067811865486830, -0.7071067811865464625, -0.000000000000000000 ) ) ;
#70558=VERTEX_POINT ( 'NONE', #98715 ) ;
#70560=VECTOR ( 'NONE', #113133, 1000.000000000000000 ) ;
#70562=ORIENTED_EDGE ( 'NONE', *, *, #48772, .T. ) ;
#70563=DIRECTION ( 'NONE',  ( 0.7071067811865487940, 0.7071067811865463515, -0.000000000000000000 ) ) ;
#70564=CARTESIAN_POINT ( 'NONE',  ( -34.49999999999975842, 22.21934299833216997, 4.348028800457638177 ) ) ;
#70565=ADVANCED_FACE ( 'NONE', ( #44386 ), #57391, .F. ) ;
#70566=FACE_BOUND ( 'NONE', #89966, .T. ) ;
#70567=EDGE_CURVE ( 'NONE', #122496, #37221, #67564, .T. ) ;
#70568=DIRECTION ( 'NONE',  ( -0.7071067811865487940, 0.7071067811865463515, -0.000000000000000000 ) ) ;
#70569=CARTESIAN_POINT ( 'NONE',  ( 0.7071067811865398012, -18.74070752338409562, 5.000000000000000000 ) ) ;
#70571=PLANE ( 'NONE',  #24903 ) ;
#70572=LINE ( 'NONE', #127778, #80599 ) ;
#70573=EDGE_LOOP ( 'NONE', ( #84408, #71754, #26283, #45702 ) ) ;
#70574=VECTOR ( 'NONE', #42226, 1000.000000000000000 ) ;
#70575=PLANE ( 'NONE',  #19399 ) ;
#70576=EDGE_CURVE ( 'NONE', #68975, #93231, #66825, .T. ) ;
#70578=ORIENTED_EDGE ( 'NONE', *, *, #53115, .F. ) ;
#70580=VERTEX_POINT ( 'NONE', #101568 ) ;
#70581=PLANE ( 'NONE',  #102239 ) ;
#70582=VECTOR ( 'NONE', #59773, 1000.000000000000000 ) ;
#70583=DIRECTION ( 'NONE',  ( 0.7071067811865486830, -0.7071067811865464625, -0.000000000000000000 ) ) ;
#70584=ORIENTED_EDGE ( 'NONE', *, *, #139680, .T. ) ;
#70585=DIRECTION ( 'NONE',  ( -0.6830127018922180770, -0.6830127018922204085, -0.2588190451025213501 ) ) ;
#70586=EDGE_CURVE ( 'NONE', #58831, #119104, #132095, .T. ) ;
#70587=CARTESIAN_POINT ( 'NONE',  ( -3.707106781186514599, -3.740707523384248390, 5.000000000000000000 ) ) ;
#70588=AXIS2_PLACEMENT_3D ( 'NONE', #99087, #143332, #132506 ) ;
#70589=CARTESIAN_POINT ( 'NONE',  ( -31.49999999999977973, 18.43112307739199451, 4.000000000000000000 ) ) ;
#70591=DIRECTION ( 'NONE',  ( -0.000000000000000000, 0.000000000000000000, 1.000000000000000000 ) ) ;
#70592=DIRECTION ( 'NONE',  ( -0.7071067811865487940, 0.7071067811865463515, 0.000000000000000000 ) ) ;
#70593=VERTEX_POINT ( 'NONE', #78414 ) ;
#70594=EDGE_CURVE ( 'NONE', #16291, #61647, #35655, .T. ) ;
#70595=ORIENTED_EDGE ( 'NONE', *, *, #92510, .T. ) ;
#70596=DIRECTION ( 'NONE',  ( 0.7071067811865486830, -0.7071067811865464625, -0.000000000000000000 ) ) ;
#70597=CARTESIAN_POINT ( 'NONE',  ( -33.48921356237309510, -27.52281430457078670, 5.000000000000000000 ) ) ;
#70599=EDGE_LOOP ( 'NONE', ( #133360, #132772, #11307, #41000 ) ) ;
#70602=PLANE ( 'NONE',  #48484 ) ;
#70603=EDGE_LOOP ( 'NONE', ( #63640, #56155, #129349, #133677 ) ) ;
#70604=CARTESIAN_POINT ( 'NONE',  ( 0.000000000000000000, 0.000000000000000000, 5.000000000000000000 ) ) ;
#70605=EDGE_CURVE ( 'NONE', #96290, #23136, #121884, .T. ) ;
#70606=VECTOR ( 'NONE', #82259, 1000.000000000000000 ) ;
#70607=DIRECTION ( 'NONE',  ( -0.000000000000000000, -0.3543493200069152693, 0.9351131265310292928 ) ) ;
#70608=AXIS2_PLACEMENT_3D ( 'NONE', #16730, #14596, #92135 ) ;
#70610=AXIS2_PLACEMENT_3D ( 'NONE', #45661, #10135, #123210 ) ;
#70611=CARTESIAN_POINT ( 'NONE',  ( 0.000000000000000000, 0.000000000000000000, 5.000000000000000000 ) ) ;
#70612=ORIENTED_EDGE ( 'NONE', *, *, #113857, .F. ) ;
#70614=CARTESIAN_POINT ( 'NONE',  ( -8.700255128608413102, -27.71228299555199825, 4.000000000000000000 ) ) ;
#70617=PLANE ( 'NONE',  #7803 ) ;
#70619=DIRECTION ( 'NONE',  ( -0.7071067811865486830, 0.7071067811865464625, 0.000000000000000000 ) ) ;
#70620=VERTEX_POINT ( 'NONE', #65424 ) ;
#70621=CARTESIAN_POINT ( 'NONE',  ( 23.03315071937583980, 7.620612595215163765, 4.000000000000000000 ) ) ;
#70622=DIRECTION ( 'NONE',  ( -0.3543493200069162685, -0.000000000000000000, -0.9351131265310288487 ) ) ;
#70626=EDGE_CURVE ( 'NONE', #53240, #18032, #10277, .T. ) ;
#70627=PLANE ( 'NONE',  #35644 ) ;
#70628=DIRECTION ( 'NONE',  ( 0.7071067811865487940, 0.7071067811865463515, 0.000000000000000000 ) ) ;
#70629=CARTESIAN_POINT ( 'NONE',  ( -57.48921356237308800, -27.52281430457095368, 5.000000000000000000 ) ) ;
#70631=CARTESIAN_POINT ( 'NONE',  ( -34.47516574401893052, 0.02806734111581892996, 4.998110765256835286 ) ) ;
#70632=LINE ( 'NONE', #90937, #100259 ) ;
#70634=CARTESIAN_POINT ( 'NONE',  ( 8.292893218813393474, 20.25929247661551713, 5.000000000000000000 ) ) ;
#70635=DIRECTION ( 'NONE',  ( -0.000000000000000000, -0.3543493200069152693, 0.9351131265310292928 ) ) ;
#70636=EDGE_LOOP ( 'NONE', ( #103593, #94821, #33096, #137641 ) ) ;
#70637=EDGE_CURVE ( 'NONE', #133903, #139608, #21876, .T. ) ;
#70639=LINE ( 'NONE', #128550, #28668 ) ;
#70642=DIRECTION ( 'NONE',  ( -0.7071067811865486830, 0.7071067811865464625, 0.000000000000000000 ) ) ;
#70644=CARTESIAN_POINT ( 'NONE',  ( -50.99451991528749062, 28.92564299267973738, 4.000000000000000000 ) ) ;
#70645=CARTESIAN_POINT ( 'NONE',  ( -11.67183060077638856, -0.7407075233842701500, 4.000000000000000000 ) ) ;
#70646=ORIENTED_EDGE ( 'NONE', *, *, #62518, .T. ) ;
#70647=DIRECTION ( 'NONE',  ( -0.3543493200069162685, -0.000000000000000000, -0.9351131265310288487 ) ) ;
#70650=CARTESIAN_POINT ( 'NONE',  ( 62.99451991528749772, 28.92564299267982264, 4.000000000000000000 ) ) ;
#70651=EDGE_CURVE ( 'NONE', #12281, #61250, #55973, .T. ) ;
#70652=ORIENTED_EDGE ( 'NONE', *, *, #105102, .T. ) ;
#70653=EDGE_CURVE ( 'NONE', #129678, #85221, #50074, .T. ) ;
#70654=EDGE_LOOP ( 'NONE', ( #131692, #91080, #138141, #106583 ) ) ;
#70655=DIRECTION ( 'NONE',  ( 0.7071067811865487940, 0.7071067811865463515, 0.000000000000000000 ) ) ;
#70656=ORIENTED_EDGE ( 'NONE', *, *, #16711, .F. ) ;
#70657=DIRECTION ( 'NONE',  ( -0.7071067811865486830, -0.7071067811865464625, 0.000000000000000000 ) ) ;
#70658=LINE ( 'NONE', #27103, #36823 ) ;
#70659=PLANE ( 'NONE',  #62790 ) ;
#70660=CARTESIAN_POINT ( 'NONE',  ( 24.29974487139158867, -27.71228299555223273, 4.000000000000000000 ) ) ;
#70661=ADVANCED_FACE ( 'NONE', ( #58125 ), #13829, .F. ) ;
#70662=CARTESIAN_POINT ( 'NONE',  ( 0.000000000000000000, 0.000000000000000000, 5.000000000000000000 ) ) ;
#70663=DIRECTION ( 'NONE',  ( -0.6830127018922181881, 0.6830127018922202975, -0.2588190451025214056 ) ) ;
#70665=EDGE_CURVE ( 'NONE', #9428, #71344, #103691, .T. ) ;
#70666=CARTESIAN_POINT ( 'NONE',  ( 50.99451991528749062, 28.92564299267973738, 4.000000000000000000 ) ) ;
#70667=CARTESIAN_POINT ( 'NONE',  ( -34.92500000000001137, -1.298069433178978382, 4.500000000000000888 ) ) ;
#70668=CARTESIAN_POINT ( 'NONE',  ( 30.18398860626900060, 28.73617430169808173, 5.000000000000000000 ) ) ;
#70669=DIRECTION ( 'NONE',  ( 0.7071067811865486830, -0.7071067811865463515, 0.000000000000000000 ) ) ;
#70671=VECTOR ( 'NONE', #44849, 1000.000000000000227 ) ;
#70672=DIRECTION ( 'NONE',  ( 0.7071067811865487940, 0.7071067811865463515, -0.000000000000000000 ) ) ;
#70673=VERTEX_POINT ( 'NONE', #39191 ) ;
#70676=CARTESIAN_POINT ( 'NONE',  ( -0.4116149059483131256, 22.22500000000000142, 4.777194822843814137 ) ) ;
#70677=VECTOR ( 'NONE', #114659, 999.9999999999998863 ) ;
#70678=DIRECTION ( 'NONE',  ( -0.000000000000000000, 0.000000000000000000, 1.000000000000000000 ) ) ;
#70679=CARTESIAN_POINT ( 'NONE',  ( -32.99999999999976552, 5.966399257802205369, 5.000000000000000000 ) ) ;
#70680=VERTEX_POINT ( 'NONE', #116006 ) ;
#70681=EDGE_CURVE ( 'NONE', #20616, #69496, #137075, .T. ) ;
#70683=VECTOR ( 'NONE', #139283, 1000.000000000000000 ) ;
#70686=CARTESIAN_POINT ( 'NONE',  ( 33.48921356237309510, -27.52281430457078670, 5.000000000000000000 ) ) ;
#70687=ORIENTED_EDGE ( 'NONE', *, *, #101732, .F. ) ;
#70688=EDGE_LOOP ( 'NONE', ( #75426, #96147, #61579, #80966 ) ) ;
#70689=PLANE ( 'NONE',  #58234 ) ;
#70690=LINE ( 'NONE', #80838, #133296 ) ;
#70691=DIRECTION ( 'NONE',  ( 1.000000000000000000, 0.000000000000000000, 0.000000000000000000 ) ) ;
#70693=DIRECTION ( 'NONE',  ( -0.7071067811865487940, 0.7071067811865463515, 0.000000000000000000 ) ) ;
#70695=ORIENTED_EDGE ( 'NONE', *, *, #133193, .F. ) ;
#70696=DIRECTION ( 'NONE',  ( -0.000000000000000000, 0.3543493200069153248, 0.9351131265310292928 ) ) ;
#70697=LINE ( 'NONE', #3924, #57033 ) ;
#70698=CARTESIAN_POINT ( 'NONE',  ( -9.826759492923502037, -22.22500000000000142, 14.51066154962963139 ) ) ;
#70699=DIRECTION ( 'NONE',  ( 0.6830127018922180770, -0.6830127018922204085, -0.2588190451025213501 ) ) ;
#70700=VECTOR ( 'NONE', #44100, 1000.000000000000000 ) ;
#70701=VERTEX_POINT ( 'NONE', #24728 ) ;
#70702=VECTOR ( 'NONE', #133004, 1000.000000000000000 ) ;
#70703=VECTOR ( 'NONE', #73768, 1000.000000000000000 ) ;
#70704=EDGE_CURVE ( 'NONE', #132568, #70259, #138503, .T. ) ;
#70705=VERTEX_POINT ( 'NONE', #36338 ) ;
#70706=VECTOR ( 'NONE', #64626, 1000.000000000000000 ) ;
#70707=CARTESIAN_POINT ( 'NONE',  ( -34.42500000000001137, 0.000000000000000000, 4.500000000000000888 ) ) ;
#70708=EDGE_CURVE ( 'NONE', #129051, #138298, #37774, .T. ) ;
#70709=LINE ( 'NONE', #93140, #95028 ) ;
#70711=DIRECTION ( 'NONE',  ( 0.7071067811865486830, -0.7071067811865464625, -0.000000000000000000 ) ) ;
#70712=ORIENTED_EDGE ( 'NONE', *, *, #23525, .T. ) ;
#70713=EDGE_LOOP ( 'NONE', ( #120593, #37317, #44882, #28797 ) ) ;
#70714=DIRECTION ( 'NONE',  ( -0.000000000000000000, -0.3543493200069152693, 0.9351131265310292928 ) ) ;
#70715=CARTESIAN_POINT ( 'NONE',  ( 45.29974487139158867, -27.71228299555237840, 4.000000000000000000 ) ) ;
#70716=EDGE_CURVE ( 'NONE', #139251, #132813, #124761, .T. ) ;
#70717=EDGE_CURVE ( 'NONE', #69036, #5408, #47266, .T. ) ;
#70718=ORIENTED_EDGE ( 'NONE', *, *, #37918, .T. ) ;
#70719=CARTESIAN_POINT ( 'NONE',  ( -34.92500000000001137, 6.662461875838927128, 4.000000000000000000 ) ) ;
#70722=CARTESIAN_POINT ( 'NONE',  ( -36.48921356237310221, -27.52281430457080802, 5.000000000000000000 ) ) ;
#70723=EDGE_CURVE ( 'NONE', #141627, #95547, #126196, .T. ) ;
#70724=FACE_BOUND ( 'NONE', #8476, .T. ) ;
#70726=CARTESIAN_POINT ( 'NONE',  ( 21.32816939922336985, -18.74070752338409207, 4.000000000000000000 ) ) ;
#70727=CARTESIAN_POINT ( 'NONE',  ( -27.70679250724057852, 20.25929247661551358, 20.83292124670821366 ) ) ;
#70728=CARTESIAN_POINT ( 'NONE',  ( -63.48921356237309510, -27.52281430457099631, 5.000000000000000000 ) ) ;
#70729=DIRECTION ( 'NONE',  ( -0.000000000000000000, 0.3543493200069153248, 0.9351131265310292928 ) ) ;
#70730=DIRECTION ( 'NONE',  ( 0.000000000000000000, -1.000000000000000000, 0.000000000000000000 ) ) ;
#70732=EDGE_CURVE ( 'NONE', #51437, #94410, #26175, .T. ) ;
#70733=ORIENTED_EDGE ( 'NONE', *, *, #11055, .T. ) ;
#70734=ORIENTED_EDGE ( 'NONE', *, *, #134822, .F. ) ;
#70736=EDGE_LOOP ( 'NONE', ( #111085, #8786, #68039, #120361 ) ) ;
#70737=DIRECTION ( 'NONE',  ( -0.7071067811865486830, 0.7071067811865464625, 0.000000000000000000 ) ) ;
#70738=LINE ( 'NONE', #103310, #14589 ) ;
#70739=EDGE_CURVE ( 'NONE', #15691, #71257, #70438, .T. ) ;
#70741=ORIENTED_EDGE ( 'NONE', *, *, #83327, .F. ) ;
#70742=CARTESIAN_POINT ( 'NONE',  ( -21.70710678118638981, -9.740707523384184441, 5.000000000000000000 ) ) ;
#70743=PLANE ( 'NONE',  #77875 ) ;
#70744=CARTESIAN_POINT ( 'NONE',  ( 21.70701326429288613, -21.74070752338406365, 4.999753212805217117 ) ) ;
#70745=CARTESIAN_POINT ( 'NONE',  ( 32.99999999999977263, -12.03360074219761700, 5.000000000000000000 ) ) ;
#70746=CARTESIAN_POINT ( 'NONE',  ( 3.183988606268992161, 28.73617430169789699, 5.000000000000000000 ) ) ;
#70747=DIRECTION ( 'NONE',  ( -0.000000000000000000, -0.3543493200069152693, 0.9351131265310292928 ) ) ;
#70748=EDGE_CURVE ( 'NONE', #55182, #33283, #135648, .T. ) ;
#70749=FACE_OUTER_BOUND ( 'NONE', #108140, .T. ) ;
#70750=ORIENTED_EDGE ( 'NONE', *, *, #24566, .T. ) ;
#70751=CARTESIAN_POINT ( 'NONE',  ( 34.45011844616451668, -1.483719188362489172, 5.000000000000000000 ) ) ;
#70753=ORIENTED_EDGE ( 'NONE', *, *, #100899, .F. ) ;
#70754=EDGE_LOOP ( 'NONE', ( #74337, #101501, #127327, #51467 ) ) ;
#70756=ADVANCED_FACE ( 'NONE', ( #15252 ), #69701, .F. ) ;
#70760=EDGE_CURVE ( 'NONE', #137485, #121162, #48638, .T. ) ;
#70763=ORIENTED_EDGE ( 'NONE', *, *, #138137, .T. ) ;
#70764=PLANE ( 'NONE',  #64180 ) ;
#70765=ORIENTED_EDGE ( 'NONE', *, *, #128418, .F. ) ;
#70766=DIRECTION ( 'NONE',  ( 0.3543493200069162685, -0.000000000000000000, -0.9351131265310288487 ) ) ;
#70767=CARTESIAN_POINT ( 'NONE',  ( -54.48921356237310221, -27.52281430457093236, 5.000000000000000000 ) ) ;
#70768=DIRECTION ( 'NONE',  ( 1.000000000000000000, 0.000000000000000000, 0.000000000000000000 ) ) ;
#70769=ORIENTED_EDGE ( 'NONE', *, *, #140432, .T. ) ;
#70770=ORIENTED_EDGE ( 'NONE', *, *, #141728, .T. ) ;
#70771=( BOUNDED_CURVE ( )  B_SPLINE_CURVE ( 3, ( #17783, #73628, #137462, #95365 ),
 .UNSPECIFIED., .F., .F. ) 
 B_SPLINE_CURVE_WITH_KNOTS ( ( 4, 4 ),
 ( 5.143245962375951663, 6.645403452391247079 ),
 .UNSPECIFIED. ) 
 CURVE ( )  GEOMETRIC_REPRESENTATION_ITEM ( )  RATIONAL_B_SPLINE_CURVE ( ( 1.000000000000000000, 0.8206354192515209478, 0.8206354192515209478, 1.000000000000000000 ) ) 
 REPRESENTATION_ITEM ( '' )  );
#70772=CARTESIAN_POINT ( 'NONE',  ( -34.42500000000001137, -13.45860074219784863, 5.000000000000000000 ) ) ;
#70773=CARTESIAN_POINT ( 'NONE',  ( 48.18398860626899705, 28.73617430169820608, 5.000000000000000000 ) ) ;
#70774=VERTEX_POINT ( 'NONE', #60247 ) ;
#70775=CARTESIAN_POINT ( 'NONE',  ( 5.999999999999955591, -18.41253812416056945, 4.000000000000000000 ) ) ;
#70776=ORIENTED_EDGE ( 'NONE', *, *, #118380, .F. ) ;
#70778=EDGE_LOOP ( 'NONE', ( #92904, #64155, #138921, #94054 ) ) ;
#70780=ORIENTED_EDGE ( 'NONE', *, *, #7979, .F. ) ;
#70781=LINE ( 'NONE', #128701, #88824 ) ;
#70784=DIRECTION ( 'NONE',  ( -0.000000000000000000, -0.3543493200069152693, 0.9351131265310292928 ) ) ;
#70785=PLANE ( 'NONE',  #118278 ) ;
#70786=ORIENTED_EDGE ( 'NONE', *, *, #97226, .F. ) ;
#70788=VECTOR ( 'NONE', #54808, 999.9999999999998863 ) ;
#70791=VECTOR ( 'NONE', #112033, 999.9999999999998863 ) ;
#70793=AXIS2_PLACEMENT_3D ( 'NONE', #92126, #114593, #59546 ) ;
#70795=EDGE_LOOP ( 'NONE', ( #40368, #15601, #84096, #123352 ) ) ;
#70796=ORIENTED_EDGE ( 'NONE', *, *, #19804, .F. ) ;
#70797=ORIENTED_EDGE ( 'NONE', *, *, #17314, .T. ) ;
#70799=DIRECTION ( 'NONE',  ( 0.000000000000000000, 0.000000000000000000, -1.000000000000000000 ) ) ;
#70801=LINE ( 'NONE', #27251, #124031 ) ;
#70802=VECTOR ( 'NONE', #24422, 1000.000000000000000 ) ;
#70803=CARTESIAN_POINT ( 'NONE',  ( -18.70612307739182967, 22.22500000000000142, 4.000000000000000000 ) ) ;
#70804=FACE_OUTER_BOUND ( 'NONE', #115293, .T. ) ;
#70807=DIRECTION ( 'NONE',  ( -0.7071067811865486830, -0.7071067811865464625, 0.000000000000000000 ) ) ;
#70810=PLANE ( 'NONE',  #44372 ) ;
#70811=LINE ( 'NONE', #93957, #34975 ) ;
#70812=ORIENTED_EDGE ( 'NONE', *, *, #47160, .F. ) ;
#70815=DIRECTION ( 'NONE',  ( -0.3543493200069162685, -0.000000000000000000, -0.9351131265310288487 ) ) ;
#70817=ORIENTED_EDGE ( 'NONE', *, *, #20748, .F. ) ;
#70818=EDGE_CURVE ( 'NONE', #56703, #71811, #5801, .T. ) ;
#70819=DIRECTION ( 'NONE',  ( -0.7071067811865486830, 0.7071067811865464625, -0.000000000000000000 ) ) ;
#70820=DIRECTION ( 'NONE',  ( -0.000000000000000000, -0.3543493200069152693, 0.9351131265310292928 ) ) ;
#70821=ORIENTED_EDGE ( 'NONE', *, *, #123500, .T. ) ;
#70822=ADVANCED_FACE ( 'NONE', ( #83414 ), #95695, .F. ) ;
#70823=DIRECTION ( 'NONE',  ( -0.6830127018922180770, -0.6830127018922204085, -0.2588190451025213501 ) ) ;
#70824=ORIENTED_EDGE ( 'NONE', *, *, #62250, .T. ) ;
#70826=ORIENTED_EDGE ( 'NONE', *, *, #31453, .F. ) ;
#70827=LINE ( 'NONE', #136758, #29046 ) ;
#70829=FACE_OUTER_BOUND ( 'NONE', #124894, .T. ) ;
#70831=VERTEX_POINT ( 'NONE', #129036 ) ;
#70832=EDGE_CURVE ( 'NONE', #85690, #28808, #52882, .T. ) ;
#70833=CARTESIAN_POINT ( 'NONE',  ( 34.92499999999998295, -18.18334561358936341, 4.500000000000000888 ) ) ;
#70834=FACE_OUTER_BOUND ( 'NONE', #6440, .T. ) ;
#70835=LINE ( 'NONE', #128755, #55385 ) ;
#70837=PLANE ( 'NONE',  #72314 ) ;
#70838=CARTESIAN_POINT ( 'NONE',  ( 5.999999999999950262, -13.39766691384882513, -10.96608748226467256 ) ) ;
#70839=ORIENTED_EDGE ( 'NONE', *, *, #124872, .T. ) ;
#70841=EDGE_CURVE ( 'NONE', #3523, #90074, #18840, .T. ) ;
#70842=LINE ( 'NONE', #101297, #9767 ) ;
#70843=ORIENTED_EDGE ( 'NONE', *, *, #34108, .F. ) ;
#70845=LINE ( 'NONE', #49814, #89430 ) ;
#70847=PLANE ( 'NONE',  #115017 ) ;
#70848=EDGE_LOOP ( 'NONE', ( #99356, #19555, #41476, #141819, #71015 ) ) ;
#70849=EDGE_CURVE ( 'NONE', #36287, #60685, #142090, .T. ) ;
#70850=CARTESIAN_POINT ( 'NONE',  ( -26.99999999999981526, -18.03360074219755660, 5.000000000000000000 ) ) ;
#70851=DIRECTION ( 'NONE',  ( -0.6830127018922180770, -0.6830127018922204085, -0.2588190451025213501 ) ) ;
#70852=DIRECTION ( 'NONE',  ( 0.7071067811865487940, 0.7071067811865463515, 0.000000000000000000 ) ) ;
#70854=FACE_OUTER_BOUND ( 'NONE', #35277, .T. ) ;
#70855=ORIENTED_EDGE ( 'NONE', *, *, #127279, .F. ) ;
#70857=EDGE_CURVE ( 'NONE', #127030, #122448, #29709, .T. ) ;
#70861=ORIENTED_EDGE ( 'NONE', *, *, #76881, .T. ) ;
#70862=AXIS2_PLACEMENT_3D ( 'NONE', #129708, #99765, #106506 ) ;
#70863=ORIENTED_EDGE ( 'NONE', *, *, #125748, .F. ) ;
#70864=VERTEX_POINT ( 'NONE', #73957 ) ;
#70866=ORIENTED_EDGE ( 'NONE', *, *, #36012, .T. ) ;
#70867=VECTOR ( 'NONE', #60179, 1000.000000000000227 ) ;
#70868=PLANE ( 'NONE',  #112346 ) ;
#70869=ADVANCED_FACE ( 'NONE', ( #19564 ), #7230, .F. ) ;
#70870=CARTESIAN_POINT ( 'NONE',  ( -42.48921356237308800, -27.52281430457085065, 5.000000000000000000 ) ) ;
#70871=DIRECTION ( 'NONE',  ( 0.7071067811865486830, -0.7071067811865464625, -0.000000000000000000 ) ) ;
#70872=CARTESIAN_POINT ( 'NONE',  ( 56.99451991528749062, 28.92564299267978001, 4.000000000000000000 ) ) ;
#70874=LINE ( 'NONE', #47019, #95411 ) ;
#70875=DIRECTION ( 'NONE',  ( 0.7071067811865486830, -0.7071067811865464625, -0.000000000000000000 ) ) ;
#70876=EDGE_CURVE ( 'NONE', #127957, #11859, #63808, .T. ) ;
#70877=EDGE_CURVE ( 'NONE', #136293, #20115, #107281, .T. ) ;
#70879=ORIENTED_EDGE ( 'NONE', *, *, #64941, .T. ) ;
#70880=VECTOR ( 'NONE', #74199, 1000.000000000000000 ) ;
#70881=DIRECTION ( 'NONE',  ( 0.3543493200069162685, -0.000000000000000000, -0.9351131265310288487 ) ) ;
#70884=EDGE_CURVE ( 'NONE', #75249, #71697, #52193, .T. ) ;
#70885=VERTEX_POINT ( 'NONE', #141343 ) ;
#70886=ORIENTED_EDGE ( 'NONE', *, *, #77335, .T. ) ;
#70887=CARTESIAN_POINT ( 'NONE',  ( 24.71757738642550351, -21.73023691814493219, 5.000000000000000888 ) ) ;
#70888=EDGE_CURVE ( 'NONE', #90217, #101026, #119562, .T. ) ;
#70889=ADVANCED_FACE ( 'NONE', ( #96378 ), #140620, .T. ) ;
#70892=AXIS2_PLACEMENT_3D ( 'NONE', #112572, #109713, #4450 ) ;
#70893=FACE_OUTER_BOUND ( 'NONE', #92538, .T. ) ;
#70894=LINE ( 'NONE', #92600, #67391 ) ;
#70895=VECTOR ( 'NONE', #14682, 1000.000000000000000 ) ;
#70896=ORIENTED_EDGE ( 'NONE', *, *, #10457, .T. ) ;
#70897=ORIENTED_EDGE ( 'NONE', *, *, #101361, .F. ) ;
#70898=EDGE_CURVE ( 'NONE', #30958, #42096, #107967, .T. ) ;
#70899=VECTOR ( 'NONE', #68893, 1000.000000000000227 ) ;
#70900=LINE ( 'NONE', #68073, #80406 ) ;
#70901=VERTEX_POINT ( 'NONE', #64501 ) ;
#70902=AXIS2_PLACEMENT_3D ( 'NONE', #55476, #137857, #82753 ) ;
#70907=DIRECTION ( 'NONE',  ( -0.000000000000000000, 0.3543493200069153248, 0.9351131265310292928 ) ) ;
#70908=DIRECTION ( 'NONE',  ( 0.7071067811865486830, -0.7071067811865464625, -0.000000000000000000 ) ) ;
#70909=CARTESIAN_POINT ( 'NONE',  ( 34.92499999999998295, -7.199905483972748321, 4.759050581649326261 ) ) ;
#70912=VERTEX_POINT ( 'NONE', #61674 ) ;
#70913=CARTESIAN_POINT ( 'NONE',  ( 0.000000000000000000, 0.000000000000000000, 5.000000000000000000 ) ) ;
#70914=CARTESIAN_POINT ( 'NONE',  ( 5.878526836628497065, -20.24070752338406720, 7.412974875817778475 ) ) ;
#70915=ORIENTED_EDGE ( 'NONE', *, *, #43594, .F. ) ;
#70916=DIRECTION ( 'NONE',  ( -0.3543493200069163240, -0.000000000000000000, 0.9351131265310288487 ) ) ;
#70917=VERTEX_POINT ( 'NONE', #105835 ) ;
#70918=ORIENTED_EDGE ( 'NONE', *, *, #42033, .F. ) ;
#70919=DIRECTION ( 'NONE',  ( 0.7071067811865486830, -0.7071067811865464625, -0.000000000000000000 ) ) ;
#70920=ORIENTED_EDGE ( 'NONE', *, *, #25216, .T. ) ;
#70921=ORIENTED_EDGE ( 'NONE', *, *, #100632, .F. ) ;
#70923=ORIENTED_EDGE ( 'NONE', *, *, #27284, .T. ) ;
#70924=EDGE_CURVE ( 'NONE', #4056, #109940, #6496, .T. ) ;
#70926=ADVANCED_FACE ( 'NONE', ( #139236 ), #39932, .F. ) ;
#70927=DIRECTION ( 'NONE',  ( 0.7071067811865487940, 0.7071067811865463515, 0.000000000000000000 ) ) ;
#70929=( BOUNDED_CURVE ( )  B_SPLINE_CURVE ( 3, ( #17751, #96725, #117765, #62025 ),
 .UNSPECIFIED., .F., .T. ) 
 B_SPLINE_CURVE_WITH_KNOTS ( ( 4, 4 ),
 ( 2.228251278275058755, 2.286295730127291037 ),
 .UNSPECIFIED. ) 
 CURVE ( )  GEOMETRIC_REPRESENTATION_ITEM ( )  RATIONAL_B_SPLINE_CURVE ( ( 1.000000000000000000, 0.9997192565072046122, 0.9997192565072046122, 1.000000000000000000 ) ) 
 REPRESENTATION_ITEM ( '' )  );
#70931=CARTESIAN_POINT ( 'NONE',  ( 3.183988606268992161, 28.73617430169789699, 5.000000000000000000 ) ) ;
#70932=CARTESIAN_POINT ( 'NONE',  ( 6.707106781186498168, -6.740707523384214639, 5.000000000000000000 ) ) ;
#70933=CARTESIAN_POINT ( 'NONE',  ( -33.48921356237309510, -27.52281430457078670, 5.000000000000000000 ) ) ;
#70934=PLANE ( 'NONE',  #80028 ) ;
#70935=VECTOR ( 'NONE', #19988, 999.9999999999998863 ) ;
#70936=CARTESIAN_POINT ( 'NONE',  ( 33.70710678118631165, 14.25929247661557042, 5.000000000000000000 ) ) ;
#70938=CARTESIAN_POINT ( 'NONE',  ( 34.45011844616451668, 4.516280811637454207, 5.000000000000000000 ) ) ;
#70939=ORIENTED_EDGE ( 'NONE', *, *, #99006, .F. ) ;
#70940=ORIENTED_EDGE ( 'NONE', *, *, #115269, .T. ) ;
#70942=DIRECTION ( 'NONE',  ( 0.3543493200069162685, -0.000000000000000000, -0.9351131265310288487 ) ) ;
#70943=VERTEX_POINT ( 'NONE', #106546 ) ;
#70944=PLANE ( 'NONE',  #67702 ) ;
#70945=PLANE ( 'NONE',  #84869 ) ;
#70946=DIRECTION ( 'NONE',  ( 0.7071067811865487940, 0.7071067811865463515, 0.000000000000000000 ) ) ;
#70947=LINE ( 'NONE', #125314, #23209 ) ;
#70948=EDGE_LOOP ( 'NONE', ( #131354, #11846, #30831, #115579 ) ) ;
#70949=PLANE ( 'NONE',  #115996 ) ;
#70950=VERTEX_POINT ( 'NONE', #40624 ) ;
#70951=( BOUNDED_CURVE ( )  B_SPLINE_CURVE ( 3, ( #111416, #136738, #112845, #102707 ),
 .UNSPECIFIED., .F., .F. ) 
 B_SPLINE_CURVE_WITH_KNOTS ( ( 4, 4 ),
 ( 1.864375635226930505, 1.933014472006549189 ),
 .UNSPECIFIED. ) 
 CURVE ( )  GEOMETRIC_REPRESENTATION_ITEM ( )  RATIONAL_B_SPLINE_CURVE ( ( 1.000000000000000000, 0.9996074310407763175, 0.9996074310407763175, 1.000000000000000000 ) ) 
 REPRESENTATION_ITEM ( '' )  );
#70952=DIRECTION ( 'NONE',  ( 0.6830127018922180770, -0.6830127018922204085, -0.2588190451025213501 ) ) ;
#70953=VECTOR ( 'NONE', #56320, 1000.000000000000000 ) ;
#70955=DIRECTION ( 'NONE',  ( -0.7071067811865487940, 0.7071067811865463515, -0.000000000000000000 ) ) ;
#70956=CARTESIAN_POINT ( 'NONE',  ( 31.49999999999977973, -5.568876922607759461, 4.000000000000000000 ) ) ;
#70957=AXIS2_PLACEMENT_3D ( 'NONE', #31648, #65008, #130260 ) ;
#70959=ORIENTED_EDGE ( 'NONE', *, *, #93459, .T. ) ;
#70961=VERTEX_POINT ( 'NONE', #10113 ) ;
#70962=DIRECTION ( 'NONE',  ( -0.7071067811865486830, -0.7071067811865464625, 0.000000000000000000 ) ) ;
#70963=CARTESIAN_POINT ( 'NONE',  ( -19.49999999999986500, 8.319652575858361487, -8.582050562765870083 ) ) ;
#70964=DIRECTION ( 'NONE',  ( 0.6830127018922180770, -0.6830127018922204085, -0.2588190451025213501 ) ) ;
#70966=EDGE_LOOP ( 'NONE', ( #34985, #126800, #78994, #125272 ) ) ;
#70967=PLANE ( 'NONE',  #110976 ) ;
#70968=LINE ( 'NONE', #105683, #110503 ) ;
#70969=DIRECTION ( 'NONE',  ( 0.7071067811865487940, 0.7071067811865463515, -0.000000000000000000 ) ) ;
#70972=CARTESIAN_POINT ( 'NONE',  ( 34.49999999999975842, -8.945670655168960650, 4.994342998332163219 ) ) ;
#70973=VERTEX_POINT ( 'NONE', #76098 ) ;
#70974=FACE_OUTER_BOUND ( 'NONE', #61861, .T. ) ;
#70975=LINE ( 'NONE', #73813, #107231 ) ;
#70976=VERTEX_POINT ( 'NONE', #121717 ) ;
#70977=EDGE_CURVE ( 'NONE', #103327, #121984, #87681, .T. ) ;
#70978=DIRECTION ( 'NONE',  ( -0.000000000000000000, 0.3543493200069153248, 0.9351131265310292928 ) ) ;
#70980=ORIENTED_EDGE ( 'NONE', *, *, #72057, .F. ) ;
#70982=EDGE_LOOP ( 'NONE', ( #67420, #141268, #121664, #52894 ) ) ;
#70984=EDGE_CURVE ( 'NONE', #138636, #86181, #45637, .T. ) ;
#70985=DIRECTION ( 'NONE',  ( -0.7071067811865487940, 0.7071067811865463515, -0.000000000000000000 ) ) ;
#70986=DIRECTION ( 'NONE',  ( 0.7071067811865487940, 0.7071067811865463515, 0.000000000000000000 ) ) ;
#70987=LINE ( 'NONE', #4203, #46066 ) ;
#70988=VERTEX_POINT ( 'NONE', #110127 ) ;
#70989=CARTESIAN_POINT ( 'NONE',  ( 0.000000000000000000, 0.000000000000000000, 5.000000000000000000 ) ) ;
#70991=AXIS2_PLACEMENT_3D ( 'NONE', #43944, #31641, #96847 ) ;
#70992=VECTOR ( 'NONE', #37341, 999.9999999999998863 ) ;
#70993=EDGE_CURVE ( 'NONE', #117128, #60304, #121017, .T. ) ;
#70994=ADVANCED_FACE ( 'NONE', ( #78981 ), #21713, .F. ) ;
#70995=FACE_OUTER_BOUND ( 'NONE', #126455, .T. ) ;
#70996=CARTESIAN_POINT ( 'NONE',  ( 15.29974487139158867, -27.71228299555216879, 4.000000000000000000 ) ) ;
#70997=VECTOR ( 'NONE', #100562, 1000.000000000000000 ) ;
#70999=PLANE ( 'NONE',  #106402 ) ;
#71000=EDGE_CURVE ( 'NONE', #65622, #43439, #78253, .T. ) ;
#71001=FACE_OUTER_BOUND ( 'NONE', #42815, .T. ) ;
#71002=DIRECTION ( 'NONE',  ( 0.7071067811865486830, -0.7071067811865464625, -0.000000000000000000 ) ) ;
#71003=FACE_OUTER_BOUND ( 'NONE', #114097, .T. ) ;
#71006=DIRECTION ( 'NONE',  ( -0.7071067811865486830, -0.7071067811865464625, 0.000000000000000000 ) ) ;
#71007=AXIS2_PLACEMENT_3D ( 'NONE', #122308, #99870, #110709 ) ;
#71008=DIRECTION ( 'NONE',  ( -0.7071067811865486830, -0.7071067811865464625, 0.000000000000000000 ) ) ;
#71011=ORIENTED_EDGE ( 'NONE', *, *, #121223, .T. ) ;
#71013=EDGE_CURVE ( 'NONE', #8528, #19998, #32608, .T. ) ;
#71014=EDGE_LOOP ( 'NONE', ( #38138, #106331, #80689, #133823 ) ) ;
#71015=ORIENTED_EDGE ( 'NONE', *, *, #58721, .F. ) ;
#71017=EDGE_CURVE ( 'NONE', #36186, #127483, #12254, .T. ) ;
#71018=LINE ( 'NONE', #83302, #13924 ) ;
#71019=FACE_OUTER_BOUND ( 'NONE', #73814, .T. ) ;
#71021=EDGE_CURVE ( 'NONE', #134912, #142570, #65970, .T. ) ;
#71022=DIRECTION ( 'NONE',  ( -0.7071067811865486830, -0.7071067811865464625, 0.000000000000000000 ) ) ;
#71023=DIRECTION ( 'NONE',  ( 0.6830127018922181881, 0.6830127018922202975, -0.2588190451025214056 ) ) ;
#71024=CARTESIAN_POINT ( 'NONE',  ( 3.489213562373097322, -27.52281430457057709, 5.000000000000000000 ) ) ;
#71026=CARTESIAN_POINT ( 'NONE',  ( -12.00548008471251293, 28.92564299267929684, 4.000000000000000000 ) ) ;
#71027=CARTESIAN_POINT ( 'NONE',  ( 12.29974487139158512, -27.71228299555214747, 4.000000000000000000 ) ) ;
#71029=EDGE_CURVE ( 'NONE', #131632, #67882, #120265, .T. ) ;
#71030=CARTESIAN_POINT ( 'NONE',  ( 27.48921356237309155, -27.52281430457074762, 5.000000000000000000 ) ) ;
#71031=CARTESIAN_POINT ( 'NONE',  ( -26.20710678118635428, -8.240707523384200428, 5.000000000000000000 ) ) ;
#71033=CARTESIAN_POINT ( 'NONE',  ( -0.7928932188134476533, -8.240707523384200428, 5.000000000000000000 ) ) ;
#71038=ORIENTED_EDGE ( 'NONE', *, *, #46335, .F. ) ;
#71039=EDGE_CURVE ( 'NONE', #53276, #16457, #99239, .T. ) ;
#71040=LINE ( 'NONE', #136264, #1536 ) ;
#71041=VECTOR ( 'NONE', #71213, 1000.000000000000000 ) ;
#71042=EDGE_LOOP ( 'NONE', ( #77908, #123256, #100817, #128719 ) ) ;
#71043=CARTESIAN_POINT ( 'NONE',  ( -19.17183060077633172, -17.24070752338410273, 4.000000000000000000 ) ) ;
#71044=LINE ( 'NONE', #7141, #60524 ) ;
#71045=EDGE_CURVE ( 'NONE', #141546, #142614, #65247, .T. ) ;
#71047=EDGE_LOOP ( 'NONE', ( #6086, #129785, #24878, #69316 ) ) ;
#71048=EDGE_CURVE ( 'NONE', #64057, #120574, #143481, .T. ) ;
#71049=ORIENTED_EDGE ( 'NONE', *, *, #119531, .F. ) ;
#71050=LINE ( 'NONE', #63741, #10578 ) ;
#71052=CARTESIAN_POINT ( 'NONE',  ( -34.42500000000001137, -21.02281430457035682, 5.000000000000000000 ) ) ;
#71053=DIRECTION ( 'NONE',  ( 1.000000000000000000, 0.000000000000000000, 0.000000000000000000 ) ) ;
#71054=ADVANCED_FACE ( 'NONE', ( #44202 ), #23101, .F. ) ;
#71055=EDGE_LOOP ( 'NONE', ( #134754, #78731, #117952, #60918 ) ) ;
#71056=EDGE_LOOP ( 'NONE', ( #993, #135038, #5180, #86442 ) ) ;
#71057=VECTOR ( 'NONE', #131868, 1000.000000000000000 ) ;
#71058=EDGE_LOOP ( 'NONE', ( #5012, #132653, #97119, #92106 ) ) ;
#71062=AXIS2_PLACEMENT_3D ( 'NONE', #111739, #804, #89268 ) ;
#71064=CARTESIAN_POINT ( 'NONE',  ( -57.48921356237308800, -27.52281430457095368, 5.000000000000000000 ) ) ;
#71065=ORIENTED_EDGE ( 'NONE', *, *, #71247, .T. ) ;
#71066=VECTOR ( 'NONE', #131505, 1000.000000000000227 ) ;
#71067=VERTEX_POINT ( 'NONE', #33349 ) ;
#71068=EDGE_CURVE ( 'NONE', #36186, #72918, #11511, .T. ) ;
#71069=LINE ( 'NONE', #7901, #34041 ) ;
#71071=AXIS2_PLACEMENT_3D ( 'NONE', #85778, #66896, #10349 ) ;
#71072=ORIENTED_EDGE ( 'NONE', *, *, #94822, .F. ) ;
#71073=ADVANCED_FACE ( 'NONE', ( #100713 ), #99996, .F. ) ;
#71074=DIRECTION ( 'NONE',  ( -0.7071067811865486830, 0.7071067811865464625, 0.000000000000000000 ) ) ;
#71075=LINE ( 'NONE', #70390, #46703 ) ;
#71076=VERTEX_POINT ( 'NONE', #133345 ) ;
#71077=DIRECTION ( 'NONE',  ( -0.7071067811865486830, -0.7071067811865464625, 0.000000000000000000 ) ) ;
#71078=CARTESIAN_POINT ( 'NONE',  ( 34.17183060077623225, 21.75929247661550292, 4.000000000000000000 ) ) ;
#71080=LINE ( 'NONE', #82659, #99691 ) ;
#71081=EDGE_CURVE ( 'NONE', #45528, #119529, #67384, .T. ) ;
#71082=AXIS2_PLACEMENT_3D ( 'NONE', #61622, #141276, #39133 ) ;
#71083=FACE_BOUND ( 'NONE', #74374, .T. ) ;
#71084=VERTEX_POINT ( 'NONE', #12954 ) ;
#71085=PLANE ( 'NONE',  #129079 ) ;
#71086=LINE ( 'NONE', #28282, #80505 ) ;
#71087=CARTESIAN_POINT ( 'NONE',  ( -17.67183060077634593, -3.740707523384244837, 4.000000000000000000 ) ) ;
#71088=EDGE_LOOP ( 'NONE', ( #48768, #5129, #124222, #92411 ) ) ;
#71090=ORIENTED_EDGE ( 'NONE', *, *, #59254, .F. ) ;
#71091=ORIENTED_EDGE ( 'NONE', *, *, #135977, .T. ) ;
#71092=AXIS2_PLACEMENT_3D ( 'NONE', #27168, #71411, #60562 ) ;
#71094=AXIS2_PLACEMENT_3D ( 'NONE', #121128, #132770, #34147 ) ;
#71095=AXIS2_PLACEMENT_3D ( 'NONE', #43031, #133607, #34282 ) ;
#71098=CARTESIAN_POINT ( 'NONE',  ( -14.99999999999989164, -21.41253812416053748, 4.000000000000000000 ) ) ;
#71099=DIRECTION ( 'NONE',  ( 0.7071067811865486830, -0.7071067811865464625, -0.000000000000000000 ) ) ;
#71100=LINE ( 'NONE', #115242, #45094 ) ;
#71101=AXIS2_PLACEMENT_3D ( 'NONE', #52104, #41220, #86172 ) ;
#71102=ORIENTED_EDGE ( 'NONE', *, *, #90641, .F. ) ;
#71103=FACE_OUTER_BOUND ( 'NONE', #46394, .T. ) ;
#71105=AXIS2_PLACEMENT_3D ( 'NONE', #92214, #91533, #92947 ) ;
#71107=CARTESIAN_POINT ( 'NONE',  ( 39.48921356237310221, -27.52281430457082934, 5.000000000000000000 ) ) ;
#71108=EDGE_CURVE ( 'NONE', #95610, #63299, #38307, .T. ) ;
#71109=CARTESIAN_POINT ( 'NONE',  ( 22.49999999999984723, 10.94296225409028089, -9.576120664313204855 ) ) ;
#71110=CARTESIAN_POINT ( 'NONE',  ( -36.48921356237310221, -27.52281430457080802, 5.000000000000000000 ) ) ;
#71111=CARTESIAN_POINT ( 'NONE',  ( 34.92499999999998295, 5.087954687542306509, -1.493867085284230400 ) ) ;
#71112=ORIENTED_EDGE ( 'NONE', *, *, #605, .T. ) ;
#71113=VERTEX_POINT ( 'NONE', #90552 ) ;
#71114=ORIENTED_EDGE ( 'NONE', *, *, #86497, .T. ) ;
#71115=ORIENTED_EDGE ( 'NONE', *, *, #86875, .F. ) ;
#71116=CARTESIAN_POINT ( 'NONE',  ( 0.000000000000000000, 0.000000000000000000, 5.000000000000000000 ) ) ;
#71118=VERTEX_POINT ( 'NONE', #92660 ) ;
#71119=DIRECTION ( 'NONE',  ( -0.000000000000000000, 0.3543493200069153248, 0.9351131265310292928 ) ) ;
#71120=EDGE_CURVE ( 'NONE', #288, #112494, #36888, .T. ) ;
#71121=DIRECTION ( 'NONE',  ( 0.7071067811865487940, -0.7071067811865463515, 0.000000000000000000 ) ) ;
#71122=ORIENTED_EDGE ( 'NONE', *, *, #12234, .T. ) ;
#71123=DIRECTION ( 'NONE',  ( -0.6830127018922180770, -0.6830127018922204085, -0.2588190451025213501 ) ) ;
#71124=EDGE_LOOP ( 'NONE', ( #93921, #3679, #132291, #91979 ) ) ;
#71126=CARTESIAN_POINT ( 'NONE',  ( -10.49999999999993250, -12.08601207473291161, -10.46905243149092257 ) ) ;
#71127=VECTOR ( 'NONE', #1015, 1000.000000000000000 ) ;
#71128=ORIENTED_EDGE ( 'NONE', *, *, #7143, .F. ) ;
#71130=DIRECTION ( 'NONE',  ( 0.7071067811865487940, 0.7071067811865463515, 0.000000000000000000 ) ) ;
#71133=ORIENTED_EDGE ( 'NONE', *, *, #133187, .T. ) ;
#71134=EDGE_LOOP ( 'NONE', ( #104484, #136390, #37192, #130791 ) ) ;
#71135=DIRECTION ( 'NONE',  ( 0.6830127018922180770, -0.6830127018922204085, -0.2588190451025213501 ) ) ;
#71136=ORIENTED_EDGE ( 'NONE', *, *, #108740, .F. ) ;
#71138=PLANE ( 'NONE',  #127412 ) ;
#71139=CARTESIAN_POINT ( 'NONE',  ( 66.48921356237309510, -27.52281430457101763, 5.000000000000000000 ) ) ;
#71140=LINE ( 'NONE', #124081, #2921 ) ;
#71141=DIRECTION ( 'NONE',  ( -0.000000000000000000, 0.3543493200069153248, 0.9351131265310292928 ) ) ;
#71142=VERTEX_POINT ( 'NONE', #68815 ) ;
#71143=CARTESIAN_POINT ( 'NONE',  ( 34.42499999999998295, 22.22500000000000142, 5.000000000000000000 ) ) ;
#71144=CARTESIAN_POINT ( 'NONE',  ( 34.92499999999998295, 21.72500000000000142, 5.000000000000000000 ) ) ;
#71145=CARTESIAN_POINT ( 'NONE',  ( 36.48921356237310221, -27.52281430457080802, 5.000000000000000000 ) ) ;
#71146=ADVANCED_FACE ( 'NONE', ( #81845 ), #134791, .F. ) ;
#71148=EDGE_LOOP ( 'NONE', ( #132628, #6132, #12652, #131744 ) ) ;
#71149=DIRECTION ( 'NONE',  ( 0.7071067811865487940, 0.7071067811865463515, 0.000000000000000000 ) ) ;
#71150=LINE ( 'NONE', #15279, #65471 ) ;
#71151=ORIENTED_EDGE ( 'NONE', *, *, #12893, .T. ) ;
#71152=CARTESIAN_POINT ( 'NONE',  ( -17.14994871458964809, -8.240707523384200428, 17.25253755692235558 ) ) ;
#71153=EDGE_LOOP ( 'NONE', ( #114639, #17005, #88504, #128675 ) ) ;
#71154=EDGE_CURVE ( 'NONE', #97256, #104186, #115818, .T. ) ;
#71155=EDGE_CURVE ( 'NONE', #51943, #19705, #70947, .T. ) ;
#71156=VERTEX_POINT ( 'NONE', #60070 ) ;
#71159=ORIENTED_EDGE ( 'NONE', *, *, #31470, .T. ) ;
#71160=CARTESIAN_POINT ( 'NONE',  ( 48.18398860626899705, 28.73617430169820608, 5.000000000000000000 ) ) ;
#71161=EDGE_CURVE ( 'NONE', #108305, #128690, #3494, .T. ) ;
#71162=EDGE_CURVE ( 'NONE', #102314, #58699, #110696, .T. ) ;
#71163=LINE ( 'NONE', #72619, #59009 ) ;
#71164=CARTESIAN_POINT ( 'NONE',  ( -11.99451991528749417, 28.92564299267946382, 4.000000000000000000 ) ) ;
#71165=EDGE_CURVE ( 'NONE', #47662, #14571, #69527, .T. ) ;
#71166=AXIS2_PLACEMENT_3D ( 'NONE', #18992, #139386, #86411 ) ;
#71167=VERTEX_POINT ( 'NONE', #93390 ) ;
#71168=PLANE ( 'NONE',  #73991 ) ;
#71169=DIRECTION ( 'NONE',  ( -0.7071067811865486830, 0.7071067811865464625, 0.000000000000000000 ) ) ;
#71170=EDGE_CURVE ( 'NONE', #49544, #75615, #79721, .T. ) ;
#71171=DIRECTION ( 'NONE',  ( -1.000000000000000000, 0.000000000000000000, 0.000000000000000000 ) ) ;
#71172=CARTESIAN_POINT ( 'NONE',  ( -1.433128002487412678, -21.74070752338405654, 6.915939825044077338 ) ) ;
#71173=DIRECTION ( 'NONE',  ( 0.3543493200069162685, -0.000000000000000000, -0.9351131265310288487 ) ) ;
#71174=PLANE ( 'NONE',  #138676 ) ;
#71175=EDGE_CURVE ( 'NONE', #124559, #17742, #2801, .T. ) ;
#71176=CARTESIAN_POINT ( 'NONE',  ( -34.75611968250420603, 4.705650698524018516, 4.955485411084897152 ) ) ;
#71177=VERTEX_POINT ( 'NONE', #70269 ) ;
#71178=ORIENTED_EDGE ( 'NONE', *, *, #70278, .T. ) ;
#71182=EDGE_LOOP ( 'NONE', ( #105379, #46401, #86526, #118960, #25619, #29182 ) ) ;
#71184=VERTEX_POINT ( 'NONE', #58687 ) ;
#71185=LINE ( 'NONE', #73323, #53249 ) ;
#71186=ORIENTED_EDGE ( 'NONE', *, *, #4994, .F. ) ;
#71187=FACE_OUTER_BOUND ( 'NONE', #14680, .T. ) ;
#71188=ADVANCED_FACE ( 'NONE', ( #126710 ), #123904, .F. ) ;
#71189=PLANE ( 'NONE',  #25448 ) ;
#71190=VECTOR ( 'NONE', #104916, 1000.000000000000227 ) ;
#71191=CARTESIAN_POINT ( 'NONE',  ( -17.99999999999986500, 14.96639925780211122, 5.000000000000000000 ) ) ;
#71196=CARTESIAN_POINT ( 'NONE',  ( 2.901564193917615331, 11.25929247661561305, 10.79108189686407471 ) ) ;
#71198=DIRECTION ( 'NONE',  ( -0.3543493200069162685, -0.000000000000000000, -0.9351131265310288487 ) ) ;
#71199=EDGE_CURVE ( 'NONE', #30921, #47131, #16523, .T. ) ;
#71201=CARTESIAN_POINT ( 'NONE',  ( 17.20666063542140733, 21.75929247661550292, 4.998822639870701856 ) ) ;
#71203=AXIS2_PLACEMENT_3D ( 'NONE', #46693, #79312, #122755 ) ;
#71205=CARTESIAN_POINT ( 'NONE',  ( -16.49999999999988276, -17.91344420646044000, 1.358650452708426659 ) ) ;
#71207=ORIENTED_EDGE ( 'NONE', *, *, #91985, .T. ) ;
#71208=ORIENTED_EDGE ( 'NONE', *, *, #111613, .F. ) ;
#71210=ORIENTED_EDGE ( 'NONE', *, *, #26036, .F. ) ;
#71213=DIRECTION ( 'NONE',  ( 0.7071067811865486830, -0.7071067811865464625, -0.000000000000000000 ) ) ;
#71215=DIRECTION ( 'NONE',  ( 0.7071067811865486830, -0.7071067811865464625, -0.000000000000000000 ) ) ;
#71216=CARTESIAN_POINT ( 'NONE',  ( 2.510786437626908008, -27.52281430457053446, 5.000000000000000000 ) ) ;
#71217=FACE_OUTER_BOUND ( 'NONE', #42243, .T. ) ;
#71218=ADVANCED_FACE ( 'NONE', ( #114426 ), #15095, .T. ) ;
#71220=ORIENTED_EDGE ( 'NONE', *, *, #49382, .F. ) ;
#71221=EDGE_CURVE ( 'NONE', #74158, #17485, #139049, .T. ) ;
#71222=CARTESIAN_POINT ( 'NONE',  ( 33.18398860626899705, 28.73617430169810305, 5.000000000000000000 ) ) ;
#71223=VERTEX_POINT ( 'NONE', #128866 ) ;
#71224=FACE_OUTER_BOUND ( 'NONE', #100072, .T. ) ;
#71225=CARTESIAN_POINT ( 'NONE',  ( -17.29298673570684386, -21.74070752338406720, 4.999753212805220670 ) ) ;
#71226=( BOUNDED_CURVE ( )  B_SPLINE_CURVE ( 3, ( #70744, #27919, #92433, #127217 ),
 .UNSPECIFIED., .F., .T. ) 
 B_SPLINE_CURVE_WITH_KNOTS ( ( 4, 4 ),
 ( 1.901594255663603183, 1.933014472006550966 ),
 .UNSPECIFIED. ) 
 CURVE ( )  GEOMETRIC_REPRESENTATION_ITEM ( )  RATIONAL_B_SPLINE_CURVE ( ( 1.000000000000000000, 0.9999177325257868620, 0.9999177325257868620, 1.000000000000000000 ) ) 
 REPRESENTATION_ITEM ( '' )  );
#71227=ADVANCED_FACE ( 'NONE', ( #5637 ), #143143, .T. ) ;
#71228=CARTESIAN_POINT ( 'NONE',  ( -6.707106781186487510, -15.74070752338412760, 5.000000000000000000 ) ) ;
#71229=ORIENTED_EDGE ( 'NONE', *, *, #134586, .F. ) ;
#71230=ORIENTED_EDGE ( 'NONE', *, *, #115544, .F. ) ;
#71232=DIRECTION ( 'NONE',  ( 0.3543493200069162685, -0.000000000000000000, -0.9351131265310288487 ) ) ;
#71233=CARTESIAN_POINT ( 'NONE',  ( -20.48334561358941386, 22.22500000000000142, 4.500000000000000888 ) ) ;
#71234=AXIS2_PLACEMENT_3D ( 'NONE', #55574, #97614, #141877 ) ;
#71238=ORIENTED_EDGE ( 'NONE', *, *, #127197, .T. ) ;
#71239=DIRECTION ( 'NONE',  ( -0.000000000000000000, 0.3543493200069153248, 0.9351131265310292928 ) ) ;
#71240=EDGE_CURVE ( 'NONE', #126185, #25402, #54033, .T. ) ;
#71242=VERTEX_POINT ( 'NONE', #105666 ) ;
#71243=ORIENTED_EDGE ( 'NONE', *, *, #63195, .F. ) ;
#71244=CARTESIAN_POINT ( 'NONE',  ( 34.42499999999998295, -16.45860074219779889, 5.000000000000000000 ) ) ;
#71245=ORIENTED_EDGE ( 'NONE', *, *, #43618, .F. ) ;
#71246=CARTESIAN_POINT ( 'NONE',  ( -60.18398860626900415, 28.73617430169829490, 5.000000000000000000 ) ) ;
#71247=EDGE_CURVE ( 'NONE', #119622, #118275, #17932, .T. ) ;
#71249=CARTESIAN_POINT ( 'NONE',  ( -15.18398860626900237, 28.73617430169797871, 5.000000000000000000 ) ) ;
#71250=DIRECTION ( 'NONE',  ( -0.7071067811865486830, -0.7071067811865464625, -0.000000000000000000 ) ) ;
#71251=LINE ( 'NONE', #135779, #62821 ) ;
#71252=EDGE_CURVE ( 'NONE', #110396, #140292, #10469, .T. ) ;
#71253=FACE_BOUND ( 'NONE', #85009, .T. ) ;
#71254=DIRECTION ( 'NONE',  ( -0.000000000000000000, -0.3543493200069152693, 0.9351131265310292928 ) ) ;
#71255=CARTESIAN_POINT ( 'NONE',  ( 2.999999999999981792, 14.96639925780211122, 5.000000000000000000 ) ) ;
#71256=EDGE_CURVE ( 'NONE', #81146, #79854, #65461, .T. ) ;
#71257=VERTEX_POINT ( 'NONE', #6326 ) ;
#71258=DIRECTION ( 'NONE',  ( 0.7071067811865487940, 0.7071067811865463515, 0.000000000000000000 ) ) ;
#71261=LINE ( 'NONE', #125639, #4591 ) ;
#71262=VERTEX_POINT ( 'NONE', #75764 ) ;
#71263=EDGE_CURVE ( 'NONE', #6488, #136798, #119929, .T. ) ;
#71264=EDGE_LOOP ( 'NONE', ( #14925, #32439, #56695, #128784, #129812, #60160 ) ) ;
#71266=VERTEX_POINT ( 'NONE', #22061 ) ;
#71267=VECTOR ( 'NONE', #28989, 999.9999999999998863 ) ;
#71269=CARTESIAN_POINT ( 'NONE',  ( -34.42500000000001137, 20.97718569542920264, 5.000000000000000000 ) ) ;
#71270=VERTEX_POINT ( 'NONE', #87348 ) ;
#71271=CARTESIAN_POINT ( 'NONE',  ( 17.99999999999987566, 17.96639925780207747, 5.000000000000000000 ) ) ;
#71273=VECTOR ( 'NONE', #28570, 1000.000000000000227 ) ;
#71274=EDGE_CURVE ( 'NONE', #86982, #69962, #51329, .T. ) ;
#71275=CARTESIAN_POINT ( 'NONE',  ( 14.29289321881336150, -12.74070752338415780, 5.000000000000000000 ) ) ;
#71277=CARTESIAN_POINT ( 'NONE',  ( 18.18398860626898994, 28.73617430169800002, 5.000000000000000000 ) ) ;
#71279=DIRECTION ( 'NONE',  ( 0.6830127018922180770, -0.6830127018922204085, -0.2588190451025213501 ) ) ;
#71280=ORIENTED_EDGE ( 'NONE', *, *, #85187, .T. ) ;
#71282=PLANE ( 'NONE',  #12562 ) ;
#71283=VECTOR ( 'NONE', #1864, 999.9999999999998863 ) ;
#71284=PLANE ( 'NONE',  #76761 ) ;
#71285=VERTEX_POINT ( 'NONE', #95518 ) ;
#71286=VERTEX_POINT ( 'NONE', #88058 ) ;
#71287=VECTOR ( 'NONE', #101722, 1000.000000000000000 ) ;
#71288=ORIENTED_EDGE ( 'NONE', *, *, #27824, .F. ) ;
#71289=CARTESIAN_POINT ( 'NONE',  ( 0.000000000000000000, 0.000000000000000000, 5.000000000000000000 ) ) ;
#71290=EDGE_CURVE ( 'NONE', #66060, #58311, #131564, .T. ) ;
#71291=FACE_OUTER_BOUND ( 'NONE', #81457, .T. ) ;
#71292=ORIENTED_EDGE ( 'NONE', *, *, #123182, .F. ) ;
#71293=LINE ( 'NONE', #103180, #18512 ) ;
#71294=VECTOR ( 'NONE', #52850, 1000.000000000000000 ) ;
#71298=LINE ( 'NONE', #48828, #98142 ) ;
#71299=ORIENTED_EDGE ( 'NONE', *, *, #111397, .T. ) ;
#71300=CARTESIAN_POINT ( 'NONE',  ( -14.99999999999988809, -10.06887692260770528, 4.000000000000000000 ) ) ;
#71301=DIRECTION ( 'NONE',  ( -0.7071067811865487940, 0.7071067811865463515, 0.000000000000000000 ) ) ;
#71302=PLANE ( 'NONE',  #105321 ) ;
#71303=CARTESIAN_POINT ( 'NONE',  ( -34.17183060077623225, -20.24070752338407786, 4.000000000000000000 ) ) ;
#71305=LINE ( 'NONE', #81480, #98052 ) ;
#71306=EDGE_LOOP ( 'NONE', ( #114471, #19683, #108542, #26304 ) ) ;
#71307=DIRECTION ( 'NONE',  ( 1.000000000000000000, 0.000000000000000000, 0.000000000000000000 ) ) ;
#71308=CARTESIAN_POINT ( 'NONE',  ( 23.99999999999984013, 14.87792677143811026, -11.06722581663434646 ) ) ;
#71309=CARTESIAN_POINT ( 'NONE',  ( 8.207106781186494615, 3.759292476615680112, 5.000000000000000000 ) ) ;
#71310=ORIENTED_EDGE ( 'NONE', *, *, #98636, .F. ) ;
#71311=FACE_OUTER_BOUND ( 'NONE', #35959, .T. ) ;
#71312=CARTESIAN_POINT ( 'NONE',  ( -24.29974487139158867, -27.71228299555223273, 4.000000000000000000 ) ) ;
#71313=CARTESIAN_POINT ( 'NONE',  ( -26.29289321881326913, 11.25929247661560240, 5.000000000000000000 ) ) ;
#71314=EDGE_LOOP ( 'NONE', ( #106236, #137835, #14739, #111775 ) ) ;
#71315=FACE_OUTER_BOUND ( 'NONE', #104514, .T. ) ;
#71316=CARTESIAN_POINT ( 'NONE',  ( 1.499999999999987566, -10.04351517176478303, -1.623559851933819687 ) ) ;
#71318=DIRECTION ( 'NONE',  ( 0.7071067811865487940, -0.7071067811865463515, 0.000000000000000000 ) ) ;
#71320=VERTEX_POINT ( 'NONE', #54729 ) ;
#71321=ORIENTED_EDGE ( 'NONE', *, *, #110091, .F. ) ;
#71322=VECTOR ( 'NONE', #95675, 1000.000000000000000 ) ;
#71325=DIRECTION ( 'NONE',  ( -0.000000000000000000, 0.3543493200069152138, -0.9351131265310292928 ) ) ;
#71327=LINE ( 'NONE', #115484, #96980 ) ;
#71328=LINE ( 'NONE', #16936, #78417 ) ;
#71330=EDGE_CURVE ( 'NONE', #79114, #89628, #32997, .T. ) ;
#71331=EDGE_LOOP ( 'NONE', ( #96922, #4862, #129747, #141517 ) ) ;
#71332=DIRECTION ( 'NONE',  ( -0.7071067811865486830, -0.7071067811865464625, -0.000000000000000000 ) ) ;
#71333=ADVANCED_FACE ( 'NONE', ( #138329 ), #76487, .T. ) ;
#71334=FACE_OUTER_BOUND ( 'NONE', #53426, .T. ) ;
#71336=EDGE_CURVE ( 'NONE', #107847, #125874, #116571, .T. ) ;
#71338=DIRECTION ( 'NONE',  ( -0.6830127018922181881, 0.6830127018922202975, -0.2588190451025214056 ) ) ;
#71340=ORIENTED_EDGE ( 'NONE', *, *, #87367, .F. ) ;
#71341=DIRECTION ( 'NONE',  ( -1.000000000000000000, 0.000000000000000000, -0.000000000000000000 ) ) ;
#71342=ORIENTED_EDGE ( 'NONE', *, *, #13209, .T. ) ;
#71343=EDGE_CURVE ( 'NONE', #100429, #113476, #28143, .T. ) ;
#71344=VERTEX_POINT ( 'NONE', #135843 ) ;
#71345=CARTESIAN_POINT ( 'NONE',  ( 28.49999999999979750, 7.087461875839178305, 4.000000000000000000 ) ) ;
#71346=CARTESIAN_POINT ( 'NONE',  ( -39.18398860626899705, 28.73617430169814568, 5.000000000000000000 ) ) ;
#71347=DIRECTION ( 'NONE',  ( -0.000000000000000000, -0.3543493200069152693, 0.9351131265310292928 ) ) ;
#71348=ADVANCED_FACE ( 'NONE', ( #101052 ), #35127, .F. ) ;
#71349=DIRECTION ( 'NONE',  ( -0.000000000000000000, -0.3543493200069152693, 0.9351131265310292928 ) ) ;
#71350=EDGE_CURVE ( 'NONE', #106603, #65916, #295, .T. ) ;
#71351=DIRECTION ( 'NONE',  ( 0.3543493200069162685, -0.000000000000000000, -0.9351131265310288487 ) ) ;
#71355=DIRECTION ( 'NONE',  ( -0.7071067811865486830, -0.7071067811865464625, 0.000000000000000000 ) ) ;
#71356=DIRECTION ( 'NONE',  ( -0.000000000000000000, -1.000000000000000000, -0.000000000000000000 ) ) ;
#71357=DIRECTION ( 'NONE',  ( 0.7071067811865487940, 0.7071067811865463515, 0.000000000000000000 ) ) ;
#71358=EDGE_CURVE ( 'NONE', #82218, #102711, #45299, .T. ) ;
#71361=LINE ( 'NONE', #127143, #29772 ) ;
#71362=ORIENTED_EDGE ( 'NONE', *, *, #91690, .F. ) ;
#71363=EDGE_LOOP ( 'NONE', ( #113774, #66771, #5402, #27427 ) ) ;
#71364=AXIS2_PLACEMENT_3D ( 'NONE', #16121, #103848, #114042 ) ;
#71366=DIRECTION ( 'NONE',  ( 0.000000000000000000, 0.000000000000000000, 1.000000000000000000 ) ) ;
#71367=FACE_OUTER_BOUND ( 'NONE', #21872, .T. ) ;
#71368=DIRECTION ( 'NONE',  ( -0.7071067811865486830, 0.7071067811865464625, 0.000000000000000000 ) ) ;
#71369=ORIENTED_EDGE ( 'NONE', *, *, #80924, .F. ) ;
#71371=DIRECTION ( 'NONE',  ( 0.7071067811865486830, -0.7071067811865464625, -0.000000000000000000 ) ) ;
#71373=EDGE_CURVE ( 'NONE', #128811, #31148, #80764, .T. ) ;
#71375=ORIENTED_EDGE ( 'NONE', *, *, #93325, .T. ) ;
#71376=ORIENTED_EDGE ( 'NONE', *, *, #59328, .F. ) ;
#71377=CARTESIAN_POINT ( 'NONE',  ( 8.999999999999937828, -21.03360074219752462, 5.000000000000000000 ) ) ;
#71381=LINE ( 'NONE', #30743, #32487 ) ;
#71382=DIRECTION ( 'NONE',  ( -0.000000000000000000, 0.3543493200069153248, 0.9351131265310292928 ) ) ;
#71383=LINE ( 'NONE', #140207, #52198 ) ;
#71384=ORIENTED_EDGE ( 'NONE', *, *, #65477, .F. ) ;
#71387=CARTESIAN_POINT ( 'NONE',  ( -24.51665438641027706, 22.22500000000000142, 4.500000000000000888 ) ) ;
#71388=VECTOR ( 'NONE', #70916, 1000.000000000000227 ) ;
#71389=DIRECTION ( 'NONE',  ( 0.7071067811865486830, -0.7071067811865464625, -0.000000000000000000 ) ) ;
#71390=VECTOR ( 'NONE', #53612, 1000.000000000000000 ) ;
#71391=VECTOR ( 'NONE', #3049, 999.9999999999998863 ) ;
#71392=EDGE_CURVE ( 'NONE', #68809, #141475, #58337, .T. ) ;
#71393=VERTEX_POINT ( 'NONE', #122089 ) ;
#71394=VERTEX_POINT ( 'NONE', #23501 ) ;
#71395=CARTESIAN_POINT ( 'NONE',  ( 0.000000000000000000, 0.000000000000000000, 5.000000000000000000 ) ) ;
#71396=PLANE ( 'NONE',  #62676 ) ;
#71399=LINE ( 'NONE', #61282, #54741 ) ;
#71401=ORIENTED_EDGE ( 'NONE', *, *, #51275, .T. ) ;
#71403=VECTOR ( 'NONE', #135689, 1000.000000000000000 ) ;
#71404=CARTESIAN_POINT ( 'NONE',  ( 30.71230993966007361, -21.73547319004781286, 4.999917730833663754 ) ) ;
#71406=EDGE_LOOP ( 'NONE', ( #9936, #79494, #99155, #133640 ) ) ;
#71407=VERTEX_POINT ( 'NONE', #3167 ) ;
#71409=CARTESIAN_POINT ( 'NONE',  ( 0.000000000000000000, 0.000000000000000000, 5.000000000000000000 ) ) ;
#71410=VERTEX_POINT ( 'NONE', #55433 ) ;
#71411=DIRECTION ( 'NONE',  ( -0.000000000000000000, 0.000000000000000000, 1.000000000000000000 ) ) ;
#71412=PLANE ( 'NONE',  #12319 ) ;
#71413=VECTOR ( 'NONE', #61567, 1000.000000000000000 ) ;
#71414=VECTOR ( 'NONE', #79383, 1000.000000000000000 ) ;
#71415=VECTOR ( 'NONE', #89114, 1000.000000000000000 ) ;
#71416=EDGE_CURVE ( 'NONE', #139679, #100881, #96151, .T. ) ;
#71417=FACE_BOUND ( 'NONE', #92882, .T. ) ;
#71418=LINE ( 'NONE', #115573, #142756 ) ;
#71419=DIRECTION ( 'NONE',  ( -0.7071067811865486830, -0.7071067811865464625, -0.000000000000000000 ) ) ;
#71421=LINE ( 'NONE', #6815, #1777 ) ;
#71424=ORIENTED_EDGE ( 'NONE', *, *, #105476, .T. ) ;
#71425=ORIENTED_EDGE ( 'NONE', *, *, #4681, .T. ) ;
#71427=ORIENTED_EDGE ( 'NONE', *, *, #117774, .T. ) ;
#71428=DIRECTION ( 'NONE',  ( 2.781805975412905274E-17, -0.3543493200069152138, 0.9351131265310292928 ) ) ;
#71429=DIRECTION ( 'NONE',  ( -0.7071067811865487940, 0.7071067811865463515, 0.000000000000000000 ) ) ;
#71430=AXIS2_PLACEMENT_3D ( 'NONE', #30434, #72560, #39908 ) ;
#71431=VECTOR ( 'NONE', #139474, 1000.000000000000000 ) ;
#71433=ORIENTED_EDGE ( 'NONE', *, *, #131837, .F. ) ;
#71436=DIRECTION ( 'NONE',  ( 0.7071067811865486830, -0.7071067811865464625, -0.000000000000000000 ) ) ;
#71437=FACE_OUTER_BOUND ( 'NONE', #108944, .T. ) ;
#71438=ADVANCED_FACE ( 'NONE', ( #15441 ), #50978, .F. ) ;
#71439=CARTESIAN_POINT ( 'NONE',  ( 5.510786437626906675, -27.52281430457051314, 5.000000000000000000 ) ) ;
#71440=DIRECTION ( 'NONE',  ( 0.7071067811865487940, 0.7071067811865463515, 0.000000000000000000 ) ) ;
#71441=FACE_OUTER_BOUND ( 'NONE', #43383, .T. ) ;
#71442=CARTESIAN_POINT ( 'NONE',  ( -13.49999999999990763, -8.568876922607724822, 4.000000000000000000 ) ) ;
#71443=CARTESIAN_POINT ( 'NONE',  ( -34.75611968250421313, -9.187065745292532171, 4.955485411084894487 ) ) ;
#71444=ORIENTED_EDGE ( 'NONE', *, *, #130980, .T. ) ;
#71446=FACE_OUTER_BOUND ( 'NONE', #43441, .T. ) ;
#71448=EDGE_CURVE ( 'NONE', #134235, #16391, #84346, .T. ) ;
#71449=ORIENTED_EDGE ( 'NONE', *, *, #86580, .T. ) ;
#71451=ORIENTED_EDGE ( 'NONE', *, *, #48426, .T. ) ;
#71453=ORIENTED_EDGE ( 'NONE', *, *, #87413, .F. ) ;
#71456=VERTEX_POINT ( 'NONE', #95175 ) ;
#71457=DIRECTION ( 'NONE',  ( 0.6830127018922181881, 0.6830127018922202975, -0.2588190451025214056 ) ) ;
#71458=EDGE_LOOP ( 'NONE', ( #10059, #26210, #45629, #19094, #78076 ) ) ;
#71460=CARTESIAN_POINT ( 'NONE',  ( -63.29974487139158867, -27.71228299555250274, 4.000000000000000000 ) ) ;
#71461=CARTESIAN_POINT ( 'NONE',  ( 15.48921356237309510, -27.52281430457066236, 5.000000000000000000 ) ) ;
#71462=ORIENTED_EDGE ( 'NONE', *, *, #132635, .T. ) ;
#71463=EDGE_LOOP ( 'NONE', ( #85940, #137103, #123232, #74188 ) ) ;
#71464=EDGE_CURVE ( 'NONE', #115745, #118674, #40132, .T. ) ;
#71465=CARTESIAN_POINT ( 'NONE',  ( 22.49999999999985079, -20.94781430457061333, 5.000000000000000000 ) ) ;
#71467=VERTEX_POINT ( 'NONE', #137990 ) ;
#71468=DIRECTION ( 'NONE',  ( 0.7071067811865487940, 0.7071067811865463515, -0.000000000000000000 ) ) ;
#71469=ORIENTED_EDGE ( 'NONE', *, *, #8506, .F. ) ;
#71470=ORIENTED_EDGE ( 'NONE', *, *, #108525, .T. ) ;
#71472=VERTEX_POINT ( 'NONE', #92310 ) ;
#71473=LINE ( 'NONE', #126543, #49519 ) ;
#71474=VECTOR ( 'NONE', #36133, 999.9999999999998863 ) ;
#71475=VECTOR ( 'NONE', #25099, 1000.000000000000000 ) ;
#71476=AXIS2_PLACEMENT_3D ( 'NONE', #129889, #110951, #20386 ) ;
#71477=CARTESIAN_POINT ( 'NONE',  ( -27.18398860626900060, 28.73617430169806042, 5.000000000000000000 ) ) ;
#71478=VECTOR ( 'NONE', #130975, 1000.000000000000000 ) ;
#71479=CARTESIAN_POINT ( 'NONE',  ( 34.92499999999998295, -7.298069433178939747, 4.500000000000000888 ) ) ;
#71480=CARTESIAN_POINT ( 'NONE',  ( -13.20450575203696886, 4.382956123802139281, 4.000000000000000000 ) ) ;
#71481=CARTESIAN_POINT ( 'NONE',  ( -60.29974487139158867, -27.71228299555248142, 4.000000000000000000 ) ) ;
#71482=ORIENTED_EDGE ( 'NONE', *, *, #111280, .T. ) ;
#71483=VECTOR ( 'NONE', #85500, 1000.000000000000000 ) ;
#71484=VECTOR ( 'NONE', #43680, 1000.000000000000000 ) ;
#71485=CARTESIAN_POINT ( 'NONE',  ( 12.18398860626900060, 28.73617430169795739, 5.000000000000000000 ) ) ;
#71487=CARTESIAN_POINT ( 'NONE',  ( 18.29974487139159223, -27.71228299555219010, 4.000000000000000000 ) ) ;
#71488=ADVANCED_FACE ( 'NONE', ( #136533 ), #5296, .F. ) ;
#71491=ORIENTED_EDGE ( 'NONE', *, *, #122579, .F. ) ;
#71492=EDGE_CURVE ( 'NONE', #45317, #40492, #37242, .T. ) ;
#71493=ORIENTED_EDGE ( 'NONE', *, *, #110930, .T. ) ;
#71494=ORIENTED_EDGE ( 'NONE', *, *, #65668, .F. ) ;
#71495=PLANE ( 'NONE',  #88067 ) ;
#71496=LINE ( 'NONE', #37443, #21051 ) ;
#71497=DIRECTION ( 'NONE',  ( 0.6830127018922181881, 0.6830127018922202975, -0.2588190451025214056 ) ) ;
#71498=AXIS2_PLACEMENT_3D ( 'NONE', #103568, #37644, #93433 ) ;
#71499=CARTESIAN_POINT ( 'NONE',  ( -11.99999999999992006, 12.83542986846996214, -1.025386466790342066 ) ) ;
#71500=CARTESIAN_POINT ( 'NONE',  ( -33.18398860626899705, 28.73617430169810305, 5.000000000000000000 ) ) ;
#71501=ADVANCED_FACE ( 'NONE', ( #139447 ), #3845, .F. ) ;
#71503=ADVANCED_FACE ( 'NONE', ( #115468 ), #14770, .F. ) ;
#71505=VECTOR ( 'NONE', #63540, 1000.000000000000227 ) ;
#71507=FACE_OUTER_BOUND ( 'NONE', #143520, .T. ) ;
#71508=LINE ( 'NONE', #69374, #78807 ) ;
#71509=CARTESIAN_POINT ( 'NONE',  ( -3.792893218813431222, -8.240707523384200428, 5.000000000000000000 ) ) ;
#71512=LINE ( 'NONE', #18514, #114732 ) ;
#71515=VECTOR ( 'NONE', #94819, 1000.000000000000000 ) ;
#71516=AXIS2_PLACEMENT_3D ( 'NONE', #30296, #42633, #109283 ) ;
#71517=DIRECTION ( 'NONE',  ( -0.6830127018922181881, 0.6830127018922202975, -0.2588190451025214056 ) ) ;
#71518=DIRECTION ( 'NONE',  ( -0.6830127018922181881, 0.6830127018922202975, -0.2588190451025214056 ) ) ;
#71519=ORIENTED_EDGE ( 'NONE', *, *, #20245, .T. ) ;
#71520=EDGE_CURVE ( 'NONE', #75908, #13355, #105339, .T. ) ;
#71521=EDGE_CURVE ( 'NONE', #73032, #137982, #26374, .T. ) ;
#71522=DIRECTION ( 'NONE',  ( -0.7071067811865487940, 0.7071067811865463515, 0.000000000000000000 ) ) ;
#71523=FACE_OUTER_BOUND ( 'NONE', #79804, .T. ) ;
#71524=VERTEX_POINT ( 'NONE', #59047 ) ;
#71525=DIRECTION ( 'NONE',  ( -0.7071067811865487940, 0.7071067811865463515, -0.000000000000000000 ) ) ;
#71526=ORIENTED_EDGE ( 'NONE', *, *, #35692, .T. ) ;
#71529=AXIS2_PLACEMENT_3D ( 'NONE', #66014, #110877, #109485 ) ;
#71530=VECTOR ( 'NONE', #7933, 1000.000000000000000 ) ;
#71531=CARTESIAN_POINT ( 'NONE',  ( 14.99999999999989342, -21.84840872380823384, 2.849755605029642869 ) ) ;
#71536=ORIENTED_EDGE ( 'NONE', *, *, #48253, .F. ) ;
#71538=DIRECTION ( 'NONE',  ( 0.6830127018922181881, 0.6830127018922202975, -0.2588190451025214056 ) ) ;
#71540=DIRECTION ( 'NONE',  ( 0.7071067811865487940, -0.7071067811865463515, 0.000000000000000000 ) ) ;
#71543=LINE ( 'NONE', #41041, #79191 ) ;
#71545=CARTESIAN_POINT ( 'NONE',  ( 22.45764329680116234, -1.725981765586488192, 4.380536896699297245 ) ) ;
#71546=ORIENTED_EDGE ( 'NONE', *, *, #107482, .F. ) ;
#71548=DIRECTION ( 'NONE',  ( -0.000000000000000000, 0.000000000000000000, 1.000000000000000000 ) ) ;
#71549=ADVANCED_FACE ( 'NONE', ( #127839 ), #72780, .F. ) ;
#71550=LINE ( 'NONE', #114996, #56293 ) ;
#71551=DIRECTION ( 'NONE',  ( 0.6830127018922181881, 0.6830127018922202975, -0.2588190451025214056 ) ) ;
#71552=EDGE_LOOP ( 'NONE', ( #122186, #75039, #31823, #40239 ) ) ;
#71553=CARTESIAN_POINT ( 'NONE',  ( 54.48921356237310221, -27.52281430457093236, 5.000000000000000000 ) ) ;
#71554=CARTESIAN_POINT ( 'NONE',  ( -16.49999999999988276, -10.04351517176479192, -1.623559851933863873 ) ) ;
#71555=CARTESIAN_POINT ( 'NONE',  ( -27.29974487139158512, -27.71228299555225405, 4.000000000000000000 ) ) ;
#71556=CARTESIAN_POINT ( 'NONE',  ( -21.79289321881330466, -11.24070752338416312, 5.000000000000000000 ) ) ;
#71557=CARTESIAN_POINT ( 'NONE',  ( -34.92500000000001137, -1.199905483972785181, 4.759050581649336031 ) ) ;
#71558=ORIENTED_EDGE ( 'NONE', *, *, #71689, .F. ) ;
#71559=EDGE_CURVE ( 'NONE', #87588, #88391, #97285, .T. ) ;
#71560=LINE ( 'NONE', #140366, #103962 ) ;
#71561=CARTESIAN_POINT ( 'NONE',  ( -19.99806943317887331, -22.22500000000000142, 4.500000000000000888 ) ) ;
#71563=ORIENTED_EDGE ( 'NONE', *, *, #112816, .F. ) ;
#71565=ORIENTED_EDGE ( 'NONE', *, *, #48619, .F. ) ;
#71568=VERTEX_POINT ( 'NONE', #87164 ) ;
#71570=DIRECTION ( 'NONE',  ( 0.7071067811865487940, 0.7071067811865463515, 0.000000000000000000 ) ) ;
#71571=CARTESIAN_POINT ( 'NONE',  ( -24.72281430457042717, -21.72500000000000142, 5.000000000000000000 ) ) ;
#71573=VERTEX_POINT ( 'NONE', #119760 ) ;
#71574=CARTESIAN_POINT ( 'NONE',  ( 5.999999999999963585, 1.761378380278687983, -6.096875308897241830 ) ) ;
#71575=CARTESIAN_POINT ( 'NONE',  ( 39.48921356237310221, -27.52281430457082934, 5.000000000000000000 ) ) ;
#71578=PLANE ( 'NONE',  #29348 ) ;
#71579=CARTESIAN_POINT ( 'NONE',  ( -34.92500000000001137, -14.33753812416085971, 4.000000000000000000 ) ) ;
#71580=AXIS2_PLACEMENT_3D ( 'NONE', #44550, #15233, #92816 ) ;
#71581=AXIS2_PLACEMENT_3D ( 'NONE', #104645, #116244, #105354 ) ;
#71582=VECTOR ( 'NONE', #2521, 1000.000000000000227 ) ;
#71584=VERTEX_POINT ( 'NONE', #21190 ) ;
#71586=DIRECTION ( 'NONE',  ( 0.3543493200069163240, -0.000000000000000000, -0.9351131265310288487 ) ) ;
#71587=EDGE_CURVE ( 'NONE', #75086, #2249, #10301, .T. ) ;
#71588=DIRECTION ( 'NONE',  ( -0.7071067811865486830, -0.7071067811865464625, 0.000000000000000000 ) ) ;
#71589=PLANE ( 'NONE',  #39298 ) ;
#71590=CARTESIAN_POINT ( 'NONE',  ( -18.28838880452753202, -2.745211937670052560, 5.000000000000000000 ) ) ;
#71591=LINE ( 'NONE', #115753, #104570 ) ;
#71593=LINE ( 'NONE', #51982, #71190 ) ;
#71594=DIRECTION ( 'NONE',  ( -0.7071067811865487940, 0.7071067811865463515, 0.000000000000000000 ) ) ;
#71597=ORIENTED_EDGE ( 'NONE', *, *, #60095, .T. ) ;
#71598=ORIENTED_EDGE ( 'NONE', *, *, #116488, .T. ) ;
#71599=ORIENTED_EDGE ( 'NONE', *, *, #80379, .F. ) ;
#71600=VECTOR ( 'NONE', #62971, 1000.000000000000000 ) ;
#71601=( BOUNDED_CURVE ( )  B_SPLINE_CURVE ( 3, ( #109178, #129491, #17857, #30185 ),
 .UNSPECIFIED., .F., .F. ) 
 B_SPLINE_CURVE_WITH_KNOTS ( ( 4, 4 ),
 ( 5.772031613926481342, 5.830584196225662375 ),
 .UNSPECIFIED. ) 
 CURVE ( )  GEOMETRIC_REPRESENTATION_ITEM ( )  RATIONAL_B_SPLINE_CURVE ( ( 1.000000000000000000, 0.9997143199977724937, 0.9997143199977724937, 1.000000000000000000 ) ) 
 REPRESENTATION_ITEM ( '' )  );
#71602=CARTESIAN_POINT ( 'NONE',  ( 51.18398860626899705, 28.73617430169823095, 5.000000000000000000 ) ) ;
#71603=VECTOR ( 'NONE', #28401, 1000.000000000000227 ) ;
#71605=CARTESIAN_POINT ( 'NONE',  ( -34.92500000000001137, 13.70115479773740752, 1.769996414796630058 ) ) ;
#71606=DIRECTION ( 'NONE',  ( 0.6830127018922180770, -0.6830127018922204085, -0.2588190451025213501 ) ) ;
#71607=LINE ( 'NONE', #27352, #59568 ) ;
#71608=CARTESIAN_POINT ( 'NONE',  ( -63.18398860626900415, 28.73617430169831621, 5.000000000000000000 ) ) ;
#71610=LINE ( 'NONE', #94053, #118554 ) ;
#71611=VERTEX_POINT ( 'NONE', #62573 ) ;
#71612=VECTOR ( 'NONE', #11200, 999.9999999999998863 ) ;
#71614=CARTESIAN_POINT ( 'NONE',  ( -15.70710678118643422, -18.74070752338409562, 5.000000000000000000 ) ) ;
#71615=VECTOR ( 'NONE', #18893, 1000.000000000000227 ) ;
#71616=ORIENTED_EDGE ( 'NONE', *, *, #45790, .T. ) ;
#71618=CARTESIAN_POINT ( 'NONE',  ( 0.4892135623730947680, -27.52281430457055578, 5.000000000000000000 ) ) ;
#71619=ORIENTED_EDGE ( 'NONE', *, *, #131282, .F. ) ;
#71620=ORIENTED_EDGE ( 'NONE', *, *, #37649, .T. ) ;
#71623=ORIENTED_EDGE ( 'NONE', *, *, #118284, .F. ) ;
#71624=ORIENTED_EDGE ( 'NONE', *, *, #8560, .F. ) ;
#71626=VECTOR ( 'NONE', #121445, 1000.000000000000227 ) ;
#71627=ORIENTED_EDGE ( 'NONE', *, *, #40117, .F. ) ;
#71628=VECTOR ( 'NONE', #38835, 999.9999999999998863 ) ;
#71630=DIRECTION ( 'NONE',  ( 0.7071067811865487940, -0.7071067811865463515, 0.000000000000000000 ) ) ;
#71632=LINE ( 'NONE', #136872, #132829 ) ;
#71635=PLANE ( 'NONE',  #39780 ) ;
#71637=VECTOR ( 'NONE', #34959, 1000.000000000000000 ) ;
#71638=FACE_OUTER_BOUND ( 'NONE', #3840, .T. ) ;
#71639=CARTESIAN_POINT ( 'NONE',  ( -39.48921356237310221, -27.52281430457082934, 5.000000000000000000 ) ) ;
#71640=EDGE_CURVE ( 'NONE', #116493, #95953, #20457, .T. ) ;
#71641=CARTESIAN_POINT ( 'NONE',  ( -4.499999999999968914, -1.592773361805379428, -6.492772025301219330 ) ) ;
#71643=ORIENTED_EDGE ( 'NONE', *, *, #111996, .T. ) ;
#71644=PLANE ( 'NONE',  #138654 ) ;
#71645=DIRECTION ( 'NONE',  ( -0.000000000000000000, 0.3543493200069153248, 0.9351131265310292928 ) ) ;
#71647=VERTEX_POINT ( 'NONE', #43659 ) ;
#71649=EDGE_CURVE ( 'NONE', #98924, #95164, #54561, .T. ) ;
#71651=CARTESIAN_POINT ( 'NONE',  ( -20.51078643762690490, -27.52281430457041012, 5.000000000000000000 ) ) ;
#71653=DIRECTION ( 'NONE',  ( -0.000000000000000000, 0.000000000000000000, 1.000000000000000000 ) ) ;
#71654=CARTESIAN_POINT ( 'NONE',  ( -15.19713381108422290, 7.733989266307781385, 4.000000000000000000 ) ) ;
#71656=DIRECTION ( 'NONE',  ( -0.7071067811865487940, 0.7071067811865463515, -0.000000000000000000 ) ) ;
#71657=ORIENTED_EDGE ( 'NONE', *, *, #121954, .T. ) ;
#71659=CARTESIAN_POINT ( 'NONE',  ( -11.47599861414542133, 22.03583458319438293, 4.979811245910087614 ) ) ;
#71660=LINE ( 'NONE', #61526, #129297 ) ;
#71661=FACE_OUTER_BOUND ( 'NONE', #127213, .T. ) ;
#71662=ORIENTED_EDGE ( 'NONE', *, *, #113926, .F. ) ;
#71663=ADVANCED_FACE ( 'NONE', ( #131392 ), #107484, .F. ) ;
#71664=ORIENTED_EDGE ( 'NONE', *, *, #65826, .F. ) ;
#71665=ORIENTED_EDGE ( 'NONE', *, *, #309, .T. ) ;
#71666=CARTESIAN_POINT ( 'NONE',  ( 1.566871997512565562, -21.74070752338405654, 6.915939825044070233 ) ) ;
#71667=CARTESIAN_POINT ( 'NONE',  ( 3.183988606268992161, 28.73617430169789699, 5.000000000000000000 ) ) ;
#71668=LINE ( 'NONE', #28159, #26485 ) ;
#71669=DIRECTION ( 'NONE',  ( -0.000000000000000000, 0.000000000000000000, 1.000000000000000000 ) ) ;
#71670=CARTESIAN_POINT ( 'NONE',  ( -6.475126127850423963, 14.25929247661557220, 9.797011795316622695 ) ) ;
#71671=EDGE_CURVE ( 'NONE', #75064, #100892, #95895, .T. ) ;
#71672=EDGE_CURVE ( 'NONE', #31910, #27663, #117614, .T. ) ;
#71673=CARTESIAN_POINT ( 'NONE',  ( 36.48921356237310221, -27.52281430457080802, 5.000000000000000000 ) ) ;
#71674=PLANE ( 'NONE',  #67164 ) ;
#71675=LINE ( 'NONE', #80426, #127660 ) ;
#71676=CARTESIAN_POINT ( 'NONE',  ( 26.99999999999981526, 8.966399257802175171, 5.000000000000000000 ) ) ;
#71678=CARTESIAN_POINT ( 'NONE',  ( -3.183988606268992161, 28.73617430169789699, 5.000000000000000000 ) ) ;
#71679=VECTOR ( 'NONE', #108858, 1000.000000000000000 ) ;
#71680=AXIS2_PLACEMENT_3D ( 'NONE', #95362, #6888, #39586 ) ;
#71681=VECTOR ( 'NONE', #47380, 1000.000000000000000 ) ;
#71682=LINE ( 'NONE', #7816, #118823 ) ;
#71683=ADVANCED_FACE ( 'NONE', ( #51701 ), #29207, .F. ) ;
#71684=ORIENTED_EDGE ( 'NONE', *, *, #3659, .T. ) ;
#71685=AXIS2_PLACEMENT_3D ( 'NONE', #92437, #116364, #106164 ) ;
#71686=CARTESIAN_POINT ( 'NONE',  ( 18.61838490601984830, -2.240707523384257716, 13.37739548510235110 ) ) ;
#71687=CARTESIAN_POINT ( 'NONE',  ( 9.489213562373095101, -27.52281430457062328, 5.000000000000000000 ) ) ;
#71688=EDGE_LOOP ( 'NONE', ( #125035, #90623, #130622, #126129 ) ) ;
#71689=EDGE_CURVE ( 'NONE', #123220, #117459, #142966, .T. ) ;
#71690=VERTEX_POINT ( 'NONE', #41507 ) ;
#71691=EDGE_CURVE ( 'NONE', #20060, #55296, #73450, .T. ) ;
#71692=CARTESIAN_POINT ( 'NONE',  ( 30.29974487139158867, -27.71228299555227537, 4.000000000000000000 ) ) ;
#71693=FACE_OUTER_BOUND ( 'NONE', #113364, .T. ) ;
#71694=VERTEX_POINT ( 'NONE', #74895 ) ;
#71696=VECTOR ( 'NONE', #59419, 1000.000000000000000 ) ;
#71697=VERTEX_POINT ( 'NONE', #140140 ) ;
#71698=CARTESIAN_POINT ( 'NONE',  ( 69.18398860626899705, 28.73617430169835529, 5.000000000000000000 ) ) ;
#71701=ADVANCED_FACE ( 'NONE', ( #85017 ), #129225, .F. ) ;
#71702=DIRECTION ( 'NONE',  ( -0.7071067811865486830, 0.7071067811865464625, 0.000000000000000000 ) ) ;
#71703=ADVANCED_FACE ( 'NONE', ( #119068 ), #79911, .T. ) ;
#71706=CARTESIAN_POINT ( 'NONE',  ( -35.99451991528749772, 28.92564299267963079, 4.000000000000000000 ) ) ;
#71707=LINE ( 'NONE', #93447, #106140 ) ;
#71711=DIRECTION ( 'NONE',  ( 0.7071067811865487940, 0.7071067811865463515, -0.000000000000000000 ) ) ;
#71712=AXIS2_PLACEMENT_3D ( 'NONE', #122573, #13087, #57362 ) ;
#71713=EDGE_CURVE ( 'NONE', #44351, #93058, #77734, .T. ) ;
#71714=CARTESIAN_POINT ( 'NONE',  ( 60.18398860626900415, 28.73617430169829490, 5.000000000000000000 ) ) ;
#71716=ORIENTED_EDGE ( 'NONE', *, *, #41785, .F. ) ;
#71717=EDGE_LOOP ( 'NONE', ( #40934, #29888, #74840, #73421, #7734 ) ) ;
#71721=VERTEX_POINT ( 'NONE', #124084 ) ;
#71722=ORIENTED_EDGE ( 'NONE', *, *, #5900, .F. ) ;
#71725=EDGE_CURVE ( 'NONE', #22559, #50033, #133536, .T. ) ;
#71726=CARTESIAN_POINT ( 'NONE',  ( -8.999999999999944933, 11.58746187583914100, 4.000000000000000000 ) ) ;
#71727=VERTEX_POINT ( 'NONE', #13856 ) ;
#71728=VECTOR ( 'NONE', #32903, 999.9999999999998863 ) ;
#71729=DIRECTION ( 'NONE',  ( -0.7071067811865486830, -0.7071067811865464625, 0.000000000000000000 ) ) ;
#71730=VECTOR ( 'NONE', #45170, 999.9999999999998863 ) ;
#71731=LINE ( 'NONE', #17320, #85791 ) ;
#71733=DIRECTION ( 'NONE',  ( -0.000000000000000000, 0.3543493200069153248, 0.9351131265310292928 ) ) ;
#71735=VECTOR ( 'NONE', #136918, 1000.000000000000000 ) ;
#71738=CARTESIAN_POINT ( 'NONE',  ( -30.18398860626900060, 28.73617430169808173, 5.000000000000000000 ) ) ;
#71739=AXIS2_PLACEMENT_3D ( 'NONE', #117673, #53150, #130758 ) ;
#71741=CARTESIAN_POINT ( 'NONE',  ( -3.183988606268992161, 28.73617430169789699, 5.000000000000000000 ) ) ;
#71742=CARTESIAN_POINT ( 'NONE',  ( 12.98911971346042549, -22.02621442084248216, 4.990779571109223767 ) ) ;
#71743=CARTESIAN_POINT ( 'NONE',  ( -22.49999999999983658, -8.947814304570739452, 5.000000000000000000 ) ) ;
#71744=DIRECTION ( 'NONE',  ( 0.7071067811865487940, -0.7071067811865463515, 0.000000000000000000 ) ) ;
#71746=EDGE_CURVE ( 'NONE', #138298, #103133, #111781, .T. ) ;
#71747=ORIENTED_EDGE ( 'NONE', *, *, #48938, .T. ) ;
#71748=ORIENTED_EDGE ( 'NONE', *, *, #82483, .F. ) ;
#71750=ORIENTED_EDGE ( 'NONE', *, *, #82652, .F. ) ;
#71751=LINE ( 'NONE', #36950, #45592 ) ;
#71752=VECTOR ( 'NONE', #118570, 1000.000000000000000 ) ;
#71754=ORIENTED_EDGE ( 'NONE', *, *, #16731, .T. ) ;
#71755=EDGE_CURVE ( 'NONE', #75268, #70831, #24759, .T. ) ;
#71756=CARTESIAN_POINT ( 'NONE',  ( -21.79289321881330110, 9.759292476615616607, 5.000000000000000000 ) ) ;
#71757=CARTESIAN_POINT ( 'NONE',  ( 12.18398860626900060, 28.73617430169795739, 5.000000000000000000 ) ) ;
#71759=ORIENTED_EDGE ( 'NONE', *, *, #75394, .T. ) ;
#71760=DIRECTION ( 'NONE',  ( 0.3543493200069162685, -0.000000000000000000, -0.9351131265310288487 ) ) ;
#71762=CARTESIAN_POINT ( 'NONE',  ( -39.18398860626899705, 28.73617430169814568, 5.000000000000000000 ) ) ;
#71764=VECTOR ( 'NONE', #79347, 999.9999999999998863 ) ;
#71765=DIRECTION ( 'NONE',  ( 0.7071067811865487940, 0.7071067811865463515, -0.000000000000000000 ) ) ;
#71766=DIRECTION ( 'NONE',  ( -0.7071067811865487940, 0.7071067811865463515, 0.000000000000000000 ) ) ;
#71767=VERTEX_POINT ( 'NONE', #844 ) ;
#71769=ORIENTED_EDGE ( 'NONE', *, *, #100267, .F. ) ;
#71774=CARTESIAN_POINT ( 'NONE',  ( 32.99999999999977973, -6.033600742197672950, 5.000000000000000000 ) ) ;
#71775=ORIENTED_EDGE ( 'NONE', *, *, #19114, .F. ) ;
#71776=ORIENTED_EDGE ( 'NONE', *, *, #135256, .F. ) ;
#71777=LINE ( 'NONE', #52831, #52538 ) ;
#71778=ORIENTED_EDGE ( 'NONE', *, *, #32080, .F. ) ;
#71779=EDGE_CURVE ( 'NONE', #50892, #114341, #69004, .T. ) ;
#71780=ORIENTED_EDGE ( 'NONE', *, *, #66011, .F. ) ;
#71782=VECTOR ( 'NONE', #138888, 1000.000000000000000 ) ;
#71783=DIRECTION ( 'NONE',  ( 0.7071067811865486830, -0.7071067811865464625, -0.000000000000000000 ) ) ;
#71784=DIRECTION ( 'NONE',  ( -0.3543493200069162685, -0.000000000000000000, -0.9351131265310288487 ) ) ;
#71787=LINE ( 'NONE', #28272, #40924 ) ;
#71788=PLANE ( 'NONE',  #6632 ) ;
#71789=AXIS2_PLACEMENT_3D ( 'NONE', #42059, #28323, #63110 ) ;
#71791=VECTOR ( 'NONE', #88435, 1000.000000000000227 ) ;
#71792=DIRECTION ( 'NONE',  ( -0.7071067811865487940, 0.7071067811865463515, -0.000000000000000000 ) ) ;
#71794=EDGE_CURVE ( 'NONE', #39262, #64959, #57417, .T. ) ;
#71795=CARTESIAN_POINT ( 'NONE',  ( -19.72673754300674531, 9.106605730562614909, 4.258036837949483733 ) ) ;
#71796=FACE_BOUND ( 'NONE', #140311, .T. ) ;
#71797=ORIENTED_EDGE ( 'NONE', *, *, #74583, .F. ) ;
#71798=CARTESIAN_POINT ( 'NONE',  ( 36.18398860626899705, 28.73617430169812437, 5.000000000000000000 ) ) ;
#71799=EDGE_CURVE ( 'NONE', #77043, #136204, #45133, .T. ) ;
#71800=CARTESIAN_POINT ( 'NONE',  ( 31.49999999999978684, 16.77039438581781994, 0.4657186855307002826 ) ) ;
#71802=DIRECTION ( 'NONE',  ( 0.3543493200069162685, -0.000000000000000000, -0.9351131265310288487 ) ) ;
#71805=VECTOR ( 'NONE', #24967, 1000.000000000000000 ) ;
#71806=( BOUNDED_CURVE ( )  B_SPLINE_CURVE ( 3, ( #19582, #140639, #121033, #42076 ),
 .UNSPECIFIED., .F., .T. ) 
 B_SPLINE_CURVE_WITH_KNOTS ( ( 4, 4 ),
 ( 1.901594255663606736, 1.933014472006568507 ),
 .UNSPECIFIED. ) 
 CURVE ( )  GEOMETRIC_REPRESENTATION_ITEM ( )  RATIONAL_B_SPLINE_CURVE ( ( 1.000000000000000000, 0.9999177325257867510, 0.9999177325257867510, 1.000000000000000000 ) ) 
 REPRESENTATION_ITEM ( '' )  );
#71807=ORIENTED_EDGE ( 'NONE', *, *, #108085, .T. ) ;
#71808=EDGE_CURVE ( 'NONE', #107846, #129409, #32812, .T. ) ;
#71809=ADVANCED_FACE ( 'NONE', ( #112490 ), #46572, .F. ) ;
#71811=VERTEX_POINT ( 'NONE', #35687 ) ;
#71812=FACE_OUTER_BOUND ( 'NONE', #51148, .T. ) ;
#71814=CARTESIAN_POINT ( 'NONE',  ( -29.99999999999979039, 1.931123077392163712, 4.000000000000000000 ) ) ;
#71818=VECTOR ( 'NONE', #22990, 1000.000000000000227 ) ;
#71819=LINE ( 'NONE', #124744, #90861 ) ;
#71820=EDGE_CURVE ( 'NONE', #55207, #94043, #21901, .T. ) ;
#71821=VECTOR ( 'NONE', #49654, 1000.000000000000000 ) ;
#71822=CARTESIAN_POINT ( 'NONE',  ( 2.700255128608413990, -27.71228299555204089, 4.000000000000000000 ) ) ;
#71823=DIRECTION ( 'NONE',  ( -0.7071067811865486830, -0.7071067811865464625, 0.000000000000000000 ) ) ;
#71824=DIRECTION ( 'NONE',  ( 0.7071067811865486830, -0.7071067811865464625, -0.000000000000000000 ) ) ;
#71825=PLANE ( 'NONE',  #3028 ) ;
#71826=EDGE_LOOP ( 'NONE', ( #51127, #94764, #81363, #87472 ) ) ;
#71827=AXIS2_PLACEMENT_3D ( 'NONE', #109847, #64218, #141788 ) ;
#71828=ORIENTED_EDGE ( 'NONE', *, *, #65072, .T. ) ;
#71829=ORIENTED_EDGE ( 'NONE', *, *, #124388, .F. ) ;
#71830=VERTEX_POINT ( 'NONE', #66149 ) ;
#71831=CARTESIAN_POINT ( 'NONE',  ( 60.18398860626900415, 28.73617430169829490, 5.000000000000000000 ) ) ;
#71832=EDGE_CURVE ( 'NONE', #83942, #123983, #74266, .T. ) ;
#71834=VECTOR ( 'NONE', #104088, 1000.000000000000000 ) ;
#71836=DIRECTION ( 'NONE',  ( 0.6830127018922181881, 0.6830127018922202975, -0.2588190451025214056 ) ) ;
#71837=CARTESIAN_POINT ( 'NONE',  ( 13.08100000000000307, 3.174999999999998046, 5.000000000000000000 ) ) ;
#71839=DIRECTION ( 'NONE',  ( 0.7071067811865487940, 0.7071067811865463515, 0.000000000000000000 ) ) ;
#71840=ORIENTED_EDGE ( 'NONE', *, *, #98195, .T. ) ;
#71841=AXIS2_PLACEMENT_3D ( 'NONE', #129849, #142177, #139334 ) ;
#71842=DIRECTION ( 'NONE',  ( 0.3543493200069162685, -0.000000000000000000, -0.9351131265310288487 ) ) ;
#71843=EDGE_CURVE ( 'NONE', #125467, #45614, #45829, .T. ) ;
#71844=ORIENTED_EDGE ( 'NONE', *, *, #113248, .T. ) ;
#71845=CARTESIAN_POINT ( 'NONE',  ( -19.49999999999986144, -17.94781430457064531, 5.000000000000000000 ) ) ;
#71846=CARTESIAN_POINT ( 'NONE',  ( -29.99999999999977973, 17.58746187583906462, 4.000000000000000000 ) ) ;
#71848=EDGE_LOOP ( 'NONE', ( #117028, #116247, #58115, #29302 ) ) ;
#71850=CARTESIAN_POINT ( 'NONE',  ( 3.328169399223500413, -21.74070752338406365, 4.000000000000000000 ) ) ;
#71851=DIRECTION ( 'NONE',  ( -0.6830127018922181881, 0.6830127018922202975, -0.2588190451025214056 ) ) ;
#71852=EDGE_LOOP ( 'NONE', ( #73480, #47905, #3993, #81626 ) ) ;
#71853=EDGE_CURVE ( 'NONE', #40909, #29037, #44411, .T. ) ;
#71854=ORIENTED_EDGE ( 'NONE', *, *, #105326, .F. ) ;
#71856=AXIS2_PLACEMENT_3D ( 'NONE', #106615, #95767, #29784 ) ;
#71857=ORIENTED_EDGE ( 'NONE', *, *, #48234, .T. ) ;
#71858=DIRECTION ( 'NONE',  ( 0.3543493200069162685, -0.000000000000000000, -0.9351131265310288487 ) ) ;
#71859=DIRECTION ( 'NONE',  ( 0.7071067811865487940, 0.7071067811865463515, 0.000000000000000000 ) ) ;
#71861=DIRECTION ( 'NONE',  ( 0.6830127018922181881, 0.6830127018922202975, -0.2588190451025214056 ) ) ;
#71862=LINE ( 'NONE', #139258, #72680 ) ;
#71864=EDGE_CURVE ( 'NONE', #31073, #117180, #79188, .T. ) ;
#71865=CARTESIAN_POINT ( 'NONE',  ( 57.48921356237308800, -27.52281430457095368, 5.000000000000000000 ) ) ;
#71866=EDGE_CURVE ( 'NONE', #142463, #98919, #68316, .T. ) ;
#71868=CARTESIAN_POINT ( 'NONE',  ( 26.99999999999980815, 18.08204922493375477, 0.9627537363044238461 ) ) ;
#71869=ORIENTED_EDGE ( 'NONE', *, *, #56184, .F. ) ;
#71871=VECTOR ( 'NONE', #55795, 1000.000000000000000 ) ;
#71872=CARTESIAN_POINT ( 'NONE',  ( 2.719980320105942262, 0.7592924766157069794, 14.27032725228009902 ) ) ;
#71873=EDGE_CURVE ( 'NONE', #139318, #4593, #125519, .T. ) ;
#71874=ORIENTED_EDGE ( 'NONE', *, *, #40070, .F. ) ;
#71875=CARTESIAN_POINT ( 'NONE',  ( -10.49999999999992539, 8.319652575858375698, -8.582050562765852320 ) ) ;
#71876=ORIENTED_EDGE ( 'NONE', *, *, #130605, .T. ) ;
#71877=ORIENTED_EDGE ( 'NONE', *, *, #121267, .T. ) ;
#71878=CARTESIAN_POINT ( 'NONE',  ( 25.82816939922334853, -8.240707523384203981, 4.000000000000000000 ) ) ;
#71879=CARTESIAN_POINT ( 'NONE',  ( 29.99451991528749417, 28.92564299267958816, 4.000000000000000000 ) ) ;
#71880=VECTOR ( 'NONE', #51916, 1000.000000000000000 ) ;
#71881=EDGE_LOOP ( 'NONE', ( #112609, #37162, #13699, #11142 ) ) ;
#71882=CARTESIAN_POINT ( 'NONE',  ( 14.99999999999990230, 8.587461875839158765, 4.000000000000000000 ) ) ;
#71884=CARTESIAN_POINT ( 'NONE',  ( 63.18398860626900415, 28.73617430169831621, 5.000000000000000000 ) ) ;
#71885=LINE ( 'NONE', #27622, #129413 ) ;
#71886=ORIENTED_EDGE ( 'NONE', *, *, #5223, .F. ) ;
#71887=EDGE_CURVE ( 'NONE', #69437, #75364, #61701, .T. ) ;
#71888=DIRECTION ( 'NONE',  ( 0.7071067811865486830, -0.7071067811865464625, -0.000000000000000000 ) ) ;
#71889=DIRECTION ( 'NONE',  ( -0.7071067811865486830, -0.7071067811865464625, 0.000000000000000000 ) ) ;
#71890=DIRECTION ( 'NONE',  ( -0.7071067811865487940, 0.7071067811865463515, -0.000000000000000000 ) ) ;
#71891=FACE_OUTER_BOUND ( 'NONE', #64093, .T. ) ;
#71893=CARTESIAN_POINT ( 'NONE',  ( -28.82334089840009028, 5.259292476615665457, 15.86257073897104419 ) ) ;
#71894=CARTESIAN_POINT ( 'NONE',  ( -19.49999999999985079, 10.46639925780215208, 5.000000000000000000 ) ) ;
#71895=VECTOR ( 'NONE', #64359, 1000.000000000000227 ) ;
#71896=EDGE_CURVE ( 'NONE', #7006, #107344, #116036, .T. ) ;
#71897=DIRECTION ( 'NONE',  ( -0.7071067811865486830, 0.7071067811865464625, 0.000000000000000000 ) ) ;
#71901=ORIENTED_EDGE ( 'NONE', *, *, #14355, .T. ) ;
#71903=AXIS2_PLACEMENT_3D ( 'NONE', #52475, #96661, #132942 ) ;
#71905=ORIENTED_EDGE ( 'NONE', *, *, #139422, .F. ) ;
#71907=LINE ( 'NONE', #18165, #68772 ) ;
#71908=CARTESIAN_POINT ( 'NONE',  ( -33.48921356237309510, -27.52281430457078670, 5.000000000000000000 ) ) ;
#71910=VECTOR ( 'NONE', #136748, 1000.000000000000227 ) ;
#71911=AXIS2_PLACEMENT_3D ( 'NONE', #26557, #91124, #114945 ) ;
#71912=VECTOR ( 'NONE', #75492, 1000.000000000000000 ) ;
#71913=ORIENTED_EDGE ( 'NONE', *, *, #98134, .F. ) ;
#71914=CARTESIAN_POINT ( 'NONE',  ( 24.18398860626899705, 28.73617430169804265, 5.000000000000000000 ) ) ;
#71915=VECTOR ( 'NONE', #64320, 1000.000000000000000 ) ;
#71916=DIRECTION ( 'NONE',  ( 0.6830127018922180770, -0.6830127018922204085, -0.2588190451025213501 ) ) ;
#71917=PLANE ( 'NONE',  #53241 ) ;
#71918=FACE_OUTER_BOUND ( 'NONE', #103420, .T. ) ;
#71920=ORIENTED_EDGE ( 'NONE', *, *, #127314, .T. ) ;
#71922=PLANE ( 'NONE',  #67880 ) ;
#71923=CARTESIAN_POINT ( 'NONE',  ( -30.72281430457039875, -21.72499999999999432, 5.000000000000000000 ) ) ;
#71924=VECTOR ( 'NONE', #95593, 1000.000000000000000 ) ;
#71925=LINE ( 'NONE', #127713, #6045 ) ;
#71928=DIRECTION ( 'NONE',  ( -0.3543493200069162685, -0.000000000000000000, -0.9351131265310288487 ) ) ;
#71929=EDGE_CURVE ( 'NONE', #58716, #77500, #47291, .T. ) ;
#71930=ORIENTED_EDGE ( 'NONE', *, *, #48950, .T. ) ;
#71933=VERTEX_POINT ( 'NONE', #93597 ) ;
#71934=FACE_OUTER_BOUND ( 'NONE', #128272, .T. ) ;
#71935=VECTOR ( 'NONE', #105040, 999.9999999999998863 ) ;
#71936=DIRECTION ( 'NONE',  ( -0.000000000000000000, 0.3543493200069153248, 0.9351131265310292928 ) ) ;
#71937=VERTEX_POINT ( 'NONE', #37060 ) ;
#71938=CARTESIAN_POINT ( 'NONE',  ( 34.92499999999998295, -19.29806943317882784, 4.500000000000000888 ) ) ;
#71940=LINE ( 'NONE', #48038, #139335 ) ;
#71941=DIRECTION ( 'NONE',  ( -0.000000000000000000, -0.3543493200069152693, 0.9351131265310292928 ) ) ;
#71942=AXIS2_PLACEMENT_3D ( 'NONE', #27686, #4443, #72688 ) ;
#71943=AXIS2_PLACEMENT_3D ( 'NONE', #8784, #97240, #99386 ) ;
#71945=VERTEX_POINT ( 'NONE', #25458 ) ;
#71946=AXIS2_PLACEMENT_3D ( 'NONE', #47341, #91510, #135721 ) ;
#71947=PLANE ( 'NONE',  #34056 ) ;
#71948=ORIENTED_EDGE ( 'NONE', *, *, #17999, .T. ) ;
#71950=AXIS2_PLACEMENT_3D ( 'NONE', #27097, #71338, #25667 ) ;
#71952=CARTESIAN_POINT ( 'NONE',  ( 14.27718569542929572, -21.72500000000000142, 5.000000000000000000 ) ) ;
#71954=VERTEX_POINT ( 'NONE', #28346 ) ;
#71956=ORIENTED_EDGE ( 'NONE', *, *, #63275, .F. ) ;
#71957=AXIS2_PLACEMENT_3D ( 'NONE', #4561, #129246, #59752 ) ;
#71958=PLANE ( 'NONE',  #91042 ) ;
#71959=DIRECTION ( 'NONE',  ( -0.000000000000000000, -0.3543493200069152693, 0.9351131265310292928 ) ) ;
#71960=CARTESIAN_POINT ( 'NONE',  ( 8.999999999999937828, 12.83542986846997813, -1.025386466790390694 ) ) ;
#71961=CARTESIAN_POINT ( 'NONE',  ( 32.24139925780183091, 21.72499999999999432, 5.000000000000000000 ) ) ;
#71962=VECTOR ( 'NONE', #53300, 1000.000000000000000 ) ;
#71965=DIRECTION ( 'NONE',  ( -0.7071067811865486830, -0.7071067811865464625, 0.000000000000000000 ) ) ;
#71966=CARTESIAN_POINT ( 'NONE',  ( -34.42500000000001137, 0.000000000000000000, 4.500000000000000888 ) ) ;
#71967=VERTEX_POINT ( 'NONE', #116762 ) ;
#71970=CARTESIAN_POINT ( 'NONE',  ( 7.499999999999951150, -4.796895815301009947, -3.611700055028665535 ) ) ;
#71971=VERTEX_POINT ( 'NONE', #17445 ) ;
#71973=ORIENTED_EDGE ( 'NONE', *, *, #71997, .T. ) ;
#71974=CARTESIAN_POINT ( 'NONE',  ( 33.29974487139158867, -27.71228299555229313, 4.000000000000000000 ) ) ;
#71975=EDGE_CURVE ( 'NONE', #115465, #34254, #62681, .T. ) ;
#71976=FACE_BOUND ( 'NONE', #136467, .T. ) ;
#71977=CARTESIAN_POINT ( 'NONE',  ( -34.42500000000001137, 5.977185695429358958, 5.000000000000000000 ) ) ;
#71978=ADVANCED_FACE ( 'NONE', ( #113912 ), #115291, .F. ) ;
#71979=ADVANCED_FACE ( 'NONE', ( #39216 ), #103719, .F. ) ;
#71980=DIRECTION ( 'NONE',  ( -0.6830127018922180770, -0.6830127018922204085, -0.2588190451025213501 ) ) ;
#71981=ORIENTED_EDGE ( 'NONE', *, *, #100272, .T. ) ;
#71984=EDGE_LOOP ( 'NONE', ( #126679, #102989, #140184, #73881 ) ) ;
#71985=EDGE_LOOP ( 'NONE', ( #86381, #40658, #52458, #26169 ) ) ;
#71986=VECTOR ( 'NONE', #129267, 1000.000000000000227 ) ;
#71987=VECTOR ( 'NONE', #107304, 999.9999999999998863 ) ;
#71990=EDGE_CURVE ( 'NONE', #107902, #46199, #126902, .T. ) ;
#71991=EDGE_CURVE ( 'NONE', #118884, #15218, #81310, .T. ) ;
#71992=VERTEX_POINT ( 'NONE', #37805 ) ;
#71994=ORIENTED_EDGE ( 'NONE', *, *, #90817, .T. ) ;
#71995=DIRECTION ( 'NONE',  ( 0.6830127018922181881, 0.6830127018922202975, -0.2588190451025214056 ) ) ;
#71996=CARTESIAN_POINT ( 'NONE',  ( -12.18398860626900060, 28.73617430169795739, 5.000000000000000000 ) ) ;
#71997=EDGE_CURVE ( 'NONE', #91987, #57991, #4363, .T. ) ;
#71998=ORIENTED_EDGE ( 'NONE', *, *, #134348, .F. ) ;
#71999=DIRECTION ( 'NONE',  ( 0.7071067811865487940, -0.7071067811865463515, 0.000000000000000000 ) ) ;
#72000=EDGE_CURVE ( 'NONE', #139988, #45425, #137826, .T. ) ;
#72001=VECTOR ( 'NONE', #38521, 1000.000000000000000 ) ;
#72002=VECTOR ( 'NONE', #59337, 1000.000000000000227 ) ;
#72003=EDGE_CURVE ( 'NONE', #108960, #124077, #26902, .T. ) ;
#72004=VECTOR ( 'NONE', #41086, 1000.000000000000000 ) ;
#72006=DIRECTION ( 'NONE',  ( 0.3543493200069162685, -0.000000000000000000, -0.9351131265310288487 ) ) ;
#72007=CARTESIAN_POINT ( 'NONE',  ( 29.99451991528749417, 28.92564299267958816, 4.000000000000000000 ) ) ;
#72008=LINE ( 'NONE', #114737, #132641 ) ;
#72009=CARTESIAN_POINT ( 'NONE',  ( 10.49999999999993250, 5.696342897626511359, -7.587980461218374550 ) ) ;
#72013=VECTOR ( 'NONE', #61031, 1000.000000000000000 ) ;
#72014=VERTEX_POINT ( 'NONE', #69731 ) ;
#72016=CARTESIAN_POINT ( 'NONE',  ( 27.79289321881326202, 15.75929247661555443, 5.000000000000000000 ) ) ;
#72017=DIRECTION ( 'NONE',  ( -0.7071067811865486830, -0.7071067811865464625, 0.000000000000000000 ) ) ;
#72018=ORIENTED_EDGE ( 'NONE', *, *, #87630, .F. ) ;
#72020=ORIENTED_EDGE ( 'NONE', *, *, #65636, .F. ) ;
#72021=EDGE_LOOP ( 'NONE', ( #105824, #28488, #117884, #91377 ) ) ;
#72023=FACE_OUTER_BOUND ( 'NONE', #10361, .T. ) ;
#72024=ORIENTED_EDGE ( 'NONE', *, *, #54062, .F. ) ;
#72025=VECTOR ( 'NONE', #97562, 1000.000000000000000 ) ;
#72026=FACE_OUTER_BOUND ( 'NONE', #63967, .T. ) ;
#72027=ADVANCED_FACE ( 'NONE', ( #8666 ), #19590, .F. ) ;
#72028=LINE ( 'NONE', #116208, #9968 ) ;
#72030=EDGE_LOOP ( 'NONE', ( #59211, #4198, #118447, #19332 ) ) ;
#72031=AXIS2_PLACEMENT_3D ( 'NONE', #116867, #17541, #92978 ) ;
#72032=DIRECTION ( 'NONE',  ( 0.7071067811865486830, -0.7071067811865464625, -0.000000000000000000 ) ) ;
#72034=EDGE_CURVE ( 'NONE', #71967, #118712, #118161, .T. ) ;
#72035=VECTOR ( 'NONE', #63517, 1000.000000000000000 ) ;
#72036=DIRECTION ( 'NONE',  ( 0.7071067811865487940, 0.7071067811865463515, -0.000000000000000000 ) ) ;
#72037=DIRECTION ( 'NONE',  ( -0.7071067811865486830, -0.7071067811865464625, 0.000000000000000000 ) ) ;
#72038=EDGE_LOOP ( 'NONE', ( #6807, #57536, #91534, #46311 ) ) ;
#72039=CARTESIAN_POINT ( 'NONE',  ( 17.99999999999987566, 20.70535890316562799, 1.956823837851874970 ) ) ;
#72040=ORIENTED_EDGE ( 'NONE', *, *, #94496, .T. ) ;
#72041=DIRECTION ( 'NONE',  ( -0.7071067811865487940, 0.7071067811865463515, -0.000000000000000000 ) ) ;
#72042=DIRECTION ( 'NONE',  ( -0.7071067811865487940, 0.7071067811865463515, -0.000000000000000000 ) ) ;
#72044=EDGE_LOOP ( 'NONE', ( #29023, #117700, #29994, #39352, #112385 ) ) ;
#72046=EDGE_CURVE ( 'NONE', #14375, #143096, #85546, .T. ) ;
#72047=VECTOR ( 'NONE', #100270, 1000.000000000000000 ) ;
#72050=CARTESIAN_POINT ( 'NONE',  ( 20.51078643762690490, -27.52281430457041012, 5.000000000000000000 ) ) ;
#72051=DIRECTION ( 'NONE',  ( 0.6830127018922180770, -0.6830127018922204085, -0.2588190451025213501 ) ) ;
#72052=LINE ( 'NONE', #16918, #23609 ) ;
#72053=EDGE_LOOP ( 'NONE', ( #60632, #126347, #15224, #65902 ) ) ;
#72054=FACE_OUTER_BOUND ( 'NONE', #121243, .T. ) ;
#72055=VECTOR ( 'NONE', #101629, 1000.000000000000227 ) ;
#72056=CARTESIAN_POINT ( 'NONE',  ( 18.18398860626898994, 28.73617430169800002, 5.000000000000000000 ) ) ;
#72057=EDGE_CURVE ( 'NONE', #100524, #102057, #9390, .T. ) ;
#72058=FACE_OUTER_BOUND ( 'NONE', #7989, .T. ) ;
#72059=EDGE_CURVE ( 'NONE', #6489, #130351, #50805, .T. ) ;
#72060=CARTESIAN_POINT ( 'NONE',  ( -14.20666063542142687, 21.75929247661549937, 4.998822639870708073 ) ) ;
#72061=DIRECTION ( 'NONE',  ( -0.3543493200069162685, -0.000000000000000000, -0.9351131265310288487 ) ) ;
#72063=VECTOR ( 'NONE', #16009, 1000.000000000000227 ) ;
#72064=ORIENTED_EDGE ( 'NONE', *, *, #63155, .F. ) ;
#72065=DIRECTION ( 'NONE',  ( -0.6830127018922181881, 0.6830127018922202975, -0.2588190451025214056 ) ) ;
#72068=PLANE ( 'NONE',  #96817 ) ;
#72069=VECTOR ( 'NONE', #138996, 1000.000000000000227 ) ;
#72071=LINE ( 'NONE', #29930, #59900 ) ;
#72072=DIRECTION ( 'NONE',  ( -0.7071067811865486830, 0.7071067811865464625, 0.000000000000000000 ) ) ;
#72073=ORIENTED_EDGE ( 'NONE', *, *, #21095, .T. ) ;
#72074=EDGE_CURVE ( 'NONE', #31974, #57153, #29048, .T. ) ;
#72075=CARTESIAN_POINT ( 'NONE',  ( 25.49999999999982947, -2.568876922607784774, 4.000000000000000000 ) ) ;
#72076=CARTESIAN_POINT ( 'NONE',  ( 34.75611968250419181, -6.187065745292550822, 4.955485411084886493 ) ) ;
#72077=VECTOR ( 'NONE', #93290, 1000.000000000000000 ) ;
#72078=DIRECTION ( 'NONE',  ( 0.6830127018922180770, -0.6830127018922204085, -0.2588190451025213501 ) ) ;
#72080=FACE_OUTER_BOUND ( 'NONE', #89973, .T. ) ;
#72082=DIRECTION ( 'NONE',  ( -0.6830127018922180770, -0.6830127018922204085, -0.2588190451025213501 ) ) ;
#72083=EDGE_LOOP ( 'NONE', ( #56527, #140982, #89189, #53237 ) ) ;
#72085=VERTEX_POINT ( 'NONE', #76124 ) ;
#72086=ORIENTED_EDGE ( 'NONE', *, *, #45662, .F. ) ;
#72088=DIRECTION ( 'NONE',  ( 1.000000000000000000, 0.000000000000000000, 0.000000000000000000 ) ) ;
#72089=( BOUNDED_CURVE ( )  B_SPLINE_CURVE ( 3, ( #71201, #79957, #103773, #115349 ),
 .UNSPECIFIED., .F., .F. ) 
 B_SPLINE_CURVE_WITH_KNOTS ( ( 4, 4 ),
 ( 5.143245962375976532, 6.645403452391245303 ),
 .UNSPECIFIED. ) 
 CURVE ( )  GEOMETRIC_REPRESENTATION_ITEM ( )  RATIONAL_B_SPLINE_CURVE ( ( 1.000000000000000000, 0.8206354192515270540, 0.8206354192515270540, 1.000000000000000000 ) ) 
 REPRESENTATION_ITEM ( '' )  );
#72090=DIRECTION ( 'NONE',  ( 0.7071067811865487940, 0.7071067811865463515, 0.000000000000000000 ) ) ;
#72091=DIRECTION ( 'NONE',  ( 1.000000000000000000, 0.000000000000000000, 0.000000000000000000 ) ) ;
#72092=DIRECTION ( 'NONE',  ( -0.7071067811865486830, 0.7071067811865464625, 0.000000000000000000 ) ) ;
#72093=EDGE_CURVE ( 'NONE', #74972, #96881, #86992, .T. ) ;
#72094=CARTESIAN_POINT ( 'NONE',  ( 16.49999999999988987, 11.52377502935404685, -1.522421517564121363 ) ) ;
#72095=CARTESIAN_POINT ( 'NONE',  ( 34.92499999999998295, 22.22500000000000142, 4.000000000000000000 ) ) ;
#72096=VERTEX_POINT ( 'NONE', #63835 ) ;
#72097=CARTESIAN_POINT ( 'NONE',  ( 10.49999999999993250, 7.087461875839178305, 4.000000000000000000 ) ) ;
#72098=DIRECTION ( 'NONE',  ( 0.3543493200069162685, -0.000000000000000000, -0.9351131265310288487 ) ) ;
#72100=VECTOR ( 'NONE', #87046, 1000.000000000000227 ) ;
#72101=DIRECTION ( 'NONE',  ( 0.000000000000000000, -1.000000000000000000, 0.000000000000000000 ) ) ;
#72102=DIRECTION ( 'NONE',  ( -0.7071067811865486830, -0.7071067811865464625, -0.000000000000000000 ) ) ;
#72103=CARTESIAN_POINT ( 'NONE',  ( 36.18398860626899705, 28.73617430169812437, 5.000000000000000000 ) ) ;
#72105=DIRECTION ( 'NONE',  ( 0.7071067811865486830, -0.7071067811865464625, -0.000000000000000000 ) ) ;
#72106=ORIENTED_EDGE ( 'NONE', *, *, #77951, .T. ) ;
#72107=ORIENTED_EDGE ( 'NONE', *, *, #28274, .T. ) ;
#72109=DIRECTION ( 'NONE',  ( -0.7071067811865486830, -0.7071067811865464625, 0.000000000000000000 ) ) ;
#72110=FACE_OUTER_BOUND ( 'NONE', #62272, .T. ) ;
#72111=ORIENTED_EDGE ( 'NONE', *, *, #12870, .F. ) ;
#72112=EDGE_CURVE ( 'NONE', #28047, #81238, #52221, .T. ) ;
#72113=DIRECTION ( 'NONE',  ( 0.7071067811865487940, 0.7071067811865463515, 0.000000000000000000 ) ) ;
#72114=AXIS2_PLACEMENT_3D ( 'NONE', #33667, #98190, #12588 ) ;
#72115=VECTOR ( 'NONE', #30779, 1000.000000000000227 ) ;
#72116=EDGE_CURVE ( 'NONE', #133726, #22423, #84178, .T. ) ;
#72117=CARTESIAN_POINT ( 'NONE',  ( -20.51078643762690490, -27.52281430457041012, 5.000000000000000000 ) ) ;
#72119=PLANE ( 'NONE',  #48291 ) ;
#72120=EDGE_LOOP ( 'NONE', ( #123721, #75477, #131423, #93646 ) ) ;
#72121=VECTOR ( 'NONE', #141372, 999.9999999999998863 ) ;
#72122=VERTEX_POINT ( 'NONE', #97109 ) ;
#72123=VECTOR ( 'NONE', #24950, 1000.000000000000000 ) ;
#72124=VECTOR ( 'NONE', #5679, 1000.000000000000114 ) ;
#72125=VECTOR ( 'NONE', #96301, 999.9999999999998863 ) ;
#72126=CARTESIAN_POINT ( 'NONE',  ( 5.865004262483735964, 3.759292476615671230, 15.36553568819724447 ) ) ;
#72127=VECTOR ( 'NONE', #49566, 1000.000000000000227 ) ;
#72129=DIRECTION ( 'NONE',  ( 0.6830127018922181881, 0.6830127018922202975, -0.2588190451025214056 ) ) ;
#72130=CARTESIAN_POINT ( 'NONE',  ( -34.92500000000001137, -22.22500000000000142, 4.000000000000000000 ) ) ;
#72131=EDGE_CURVE ( 'NONE', #81104, #98919, #96407, .T. ) ;
#72132=CARTESIAN_POINT ( 'NONE',  ( 15.29974487139158867, -27.71228299555216879, 4.000000000000000000 ) ) ;
#72135=CARTESIAN_POINT ( 'NONE',  ( -11.99999999999991296, 12.25461709320619796, -10.07315571508699747 ) ) ;
#72136=DIRECTION ( 'NONE',  ( 0.7071067811865487940, 0.7071067811865463515, 0.000000000000000000 ) ) ;
#72139=CARTESIAN_POINT ( 'NONE',  ( 7.998069433178966570, -22.22500000000000142, 4.500000000000000888 ) ) ;
#72140=ORIENTED_EDGE ( 'NONE', *, *, #85186, .T. ) ;
#72141=ORIENTED_EDGE ( 'NONE', *, *, #138287, .T. ) ;
#72142=AXIS2_PLACEMENT_3D ( 'NONE', #33652, #110442, #53217 ) ;
#72144=CARTESIAN_POINT ( 'NONE',  ( 9.436801032208231632, -12.74070752338415247, 9.898150129686353438 ) ) ;
#72145=LINE ( 'NONE', #138804, #105747 ) ;
#72147=CARTESIAN_POINT ( 'NONE',  ( 5.999999999999956479, 10.93112307739207267, 4.000000000000000000 ) ) ;
#72149=ORIENTED_EDGE ( 'NONE', *, *, #48553, .F. ) ;
#72152=ORIENTED_EDGE ( 'NONE', *, *, #15007, .F. ) ;
#72153=VECTOR ( 'NONE', #78210, 1000.000000000000227 ) ;
#72154=ORIENTED_EDGE ( 'NONE', *, *, #2078, .T. ) ;
#72155=VECTOR ( 'NONE', #16440, 1000.000000000000000 ) ;
#72156=FACE_OUTER_BOUND ( 'NONE', #108764, .T. ) ;
#72157=VERTEX_POINT ( 'NONE', #86300 ) ;
#72158=AXIS2_PLACEMENT_3D ( 'NONE', #71289, #137965, #116907 ) ;
#72159=DIRECTION ( 'NONE',  ( 0.6830127018922180770, -0.6830127018922204085, -0.2588190451025213501 ) ) ;
#72160=PLANE ( 'NONE',  #95624 ) ;
#72161=VECTOR ( 'NONE', #78854, 1000.000000000000000 ) ;
#72162=FACE_BOUND ( 'NONE', #15211, .T. ) ;
#72163=VECTOR ( 'NONE', #36383, 1000.000000000000000 ) ;
#72164=DIRECTION ( 'NONE',  ( 1.000000000000000000, 0.000000000000000000, 0.000000000000000000 ) ) ;
#72165=EDGE_CURVE ( 'NONE', #88478, #57179, #142115, .T. ) ;
#72166=DIRECTION ( 'NONE',  ( 0.000000000000000000, 0.000000000000000000, 1.000000000000000000 ) ) ;
#72168=ORIENTED_EDGE ( 'NONE', *, *, #1438, .F. ) ;
#72169=CARTESIAN_POINT ( 'NONE',  ( 0.000000000000000000, 0.000000000000000000, 5.000000000000000000 ) ) ;
#72171=VERTEX_POINT ( 'NONE', #120292 ) ;
#72172=EDGE_CURVE ( 'NONE', #9288, #41067, #31904, .T. ) ;
#72173=EDGE_CURVE ( 'NONE', #76506, #117516, #7257, .T. ) ;
#72174=EDGE_LOOP ( 'NONE', ( #134577, #107922, #6015 ) ) ;
#72176=ORIENTED_EDGE ( 'NONE', *, *, #44024, .F. ) ;
#72177=ADVANCED_FACE ( 'NONE', ( #95725 ), #84853, .T. ) ;
#72178=CARTESIAN_POINT ( 'NONE',  ( 29.99999999999980815, 20.58746187583903264, 4.000000000000000000 ) ) ;
#72179=EDGE_CURVE ( 'NONE', #109420, #98043, #77574, .T. ) ;
#72180=AXIS2_PLACEMENT_3D ( 'NONE', #139340, #97180, #40030 ) ;
#72181=CARTESIAN_POINT ( 'NONE',  ( 53.99451991528749062, 28.92564299267975869, 4.000000000000000000 ) ) ;
#72182=AXIS2_PLACEMENT_3D ( 'NONE', #109649, #10324, #54579 ) ;
#72183=EDGE_CURVE ( 'NONE', #21250, #99801, #76869, .T. ) ;
#72184=CARTESIAN_POINT ( 'NONE',  ( -8.758305415748079525, 0.7592924766157104211, 14.37146558664984752 ) ) ;
#72185=VERTEX_POINT ( 'NONE', #89148 ) ;
#72186=CARTESIAN_POINT ( 'NONE',  ( 34.42499999999998295, 21.72500000000000142, 0.4999999999999995559 ) ) ;
#72187=EDGE_CURVE ( 'NONE', #78583, #29685, #79006, .T. ) ;
#72188=PLANE ( 'NONE',  #54707 ) ;
#72189=EDGE_CURVE ( 'NONE', #68842, #124916, #680, .T. ) ;
#72190=CARTESIAN_POINT ( 'NONE',  ( 0.000000000000000000, 0.000000000000000000, 5.000000000000000000 ) ) ;
#72191=CARTESIAN_POINT ( 'NONE',  ( -14.99451991528749595, 28.92564299267948513, 4.000000000000000000 ) ) ;
#72192=PLANE ( 'NONE',  #38098 ) ;
#72193=LINE ( 'NONE', #62716, #9867 ) ;
#72196=DIRECTION ( 'NONE',  ( 0.3543493200069162685, -0.000000000000000000, -0.9351131265310288487 ) ) ;
#72197=EDGE_LOOP ( 'NONE', ( #96348, #66401, #124324, #24919 ) ) ;
#72198=FACE_OUTER_BOUND ( 'NONE', #39024, .T. ) ;
#72199=DIRECTION ( 'NONE',  ( -0.6830127018922181881, 0.6830127018922202975, -0.2588190451025214056 ) ) ;
#72201=VERTEX_POINT ( 'NONE', #78275 ) ;
#72202=ORIENTED_EDGE ( 'NONE', *, *, #109756, .T. ) ;
#72203=EDGE_CURVE ( 'NONE', #102270, #51451, #24584, .T. ) ;
#72204=ORIENTED_EDGE ( 'NONE', *, *, #56853, .T. ) ;
#72206=VECTOR ( 'NONE', #137854, 1000.000000000000000 ) ;
#72207=ORIENTED_EDGE ( 'NONE', *, *, #99006, .T. ) ;
#72208=EDGE_CURVE ( 'NONE', #36106, #10226, #34769, .T. ) ;
#72210=( BOUNDED_CURVE ( )  B_SPLINE_CURVE ( 3, ( #75191, #64288, #18603, #131688 ),
 .UNSPECIFIED., .F., .T. ) 
 B_SPLINE_CURVE_WITH_KNOTS ( ( 4, 4 ),
 ( 5.106027341939297415, 6.645403452391245303 ),
 .UNSPECIFIED. ) 
 CURVE ( )  GEOMETRIC_REPRESENTATION_ITEM ( )  RATIONAL_B_SPLINE_CURVE ( ( 1.000000000000000000, 0.8120851936182316155, 0.8120851936182316155, 1.000000000000000000 ) ) 
 REPRESENTATION_ITEM ( '' )  );
#72212=PLANE ( 'NONE',  #3293 ) ;
#72213=VERTEX_POINT ( 'NONE', #100024 ) ;
#72214=CARTESIAN_POINT ( 'NONE',  ( -34.42500000000001137, 0.000000000000000000, 4.500000000000000888 ) ) ;
#72217=VECTOR ( 'NONE', #108683, 1000.000000000000000 ) ;
#72218=FACE_OUTER_BOUND ( 'NONE', #120328, .T. ) ;
#72219=VERTEX_POINT ( 'NONE', #87707 ) ;
#72220=ORIENTED_EDGE ( 'NONE', *, *, #95420, .T. ) ;
#72222=DIRECTION ( 'NONE',  ( 0.3543493200069162685, -0.000000000000000000, -0.9351131265310288487 ) ) ;
#72223=VECTOR ( 'NONE', #9172, 1000.000000000000114 ) ;
#72225=ORIENTED_EDGE ( 'NONE', *, *, #77218, .T. ) ;
#72226=DIRECTION ( 'NONE',  ( -0.7071067811865487940, 0.7071067811865463515, -0.000000000000000000 ) ) ;
#72227=VERTEX_POINT ( 'NONE', #110845 ) ;
#72228=ORIENTED_EDGE ( 'NONE', *, *, #83163, .F. ) ;
#72229=EDGE_LOOP ( 'NONE', ( #140291, #89220, #23968, #35319 ) ) ;
#72231=EDGE_CURVE ( 'NONE', #16928, #120251, #133373, .T. ) ;
#72232=DIRECTION ( 'NONE',  ( -0.000000000000000000, 0.000000000000000000, 1.000000000000000000 ) ) ;
#72233=VECTOR ( 'NONE', #41902, 1000.000000000000000 ) ;
#72234=AXIS2_PLACEMENT_3D ( 'NONE', #112525, #82580, #34259 ) ;
#72236=CARTESIAN_POINT ( 'NONE',  ( -7.499999999999944045, 3.073033219394612825, -6.593910359670984711 ) ) ;
#72237=CARTESIAN_POINT ( 'NONE',  ( 21.04658813629531267, 14.25929247661557042, 18.84478104361322792 ) ) ;
#72238=LINE ( 'NONE', #126546, #71782 ) ;
#72239=ORIENTED_EDGE ( 'NONE', *, *, #25090, .F. ) ;
#72241=VECTOR ( 'NONE', #85627, 1000.000000000000227 ) ;
#72242=VERTEX_POINT ( 'NONE', #55091 ) ;
#72243=DIRECTION ( 'NONE',  ( -0.7071067811865486830, 0.7071067811865464625, 0.000000000000000000 ) ) ;
#72244=EDGE_CURVE ( 'NONE', #99187, #69646, #68151, .T. ) ;
#72246=LINE ( 'NONE', #128028, #90184 ) ;
#72247=DIRECTION ( 'NONE',  ( 0.7071067811865487940, 0.7071067811865463515, 0.000000000000000000 ) ) ;
#72248=PLANE ( 'NONE',  #39698 ) ;
#72249=ORIENTED_EDGE ( 'NONE', *, *, #127156, .T. ) ;
#72250=ORIENTED_EDGE ( 'NONE', *, *, #126223, .T. ) ;
#72251=ADVANCED_FACE ( 'NONE', ( #43492 ), #11538, .F. ) ;
#72252=ORIENTED_EDGE ( 'NONE', *, *, #56322, .F. ) ;
#72253=LINE ( 'NONE', #138177, #51022 ) ;
#72254=DIRECTION ( 'NONE',  ( 0.000000000000000000, -0.3543493200069153248, -0.9351131265310292928 ) ) ;
#72255=CARTESIAN_POINT ( 'NONE',  ( 2.994519915287485734, 28.92564299267940342, 4.000000000000000000 ) ) ;
#72256=PLANE ( 'NONE',  #114515 ) ;
#72259=AXIS2_PLACEMENT_3D ( 'NONE', #122964, #111350, #92441 ) ;
#72261=VECTOR ( 'NONE', #87275, 999.9999999999998863 ) ;
#72262=CARTESIAN_POINT ( 'NONE',  ( -48.29974487139158867, -27.71228299555239971, 4.000000000000000000 ) ) ;
#72263=CARTESIAN_POINT ( 'NONE',  ( 1.499999999999990896, 6.431123077392122411, 4.000000000000000000 ) ) ;
#72265=CARTESIAN_POINT ( 'NONE',  ( -27.29974487139158512, -27.71228299555225405, 4.000000000000000000 ) ) ;
#72266=AXIS2_PLACEMENT_3D ( 'NONE', #103687, #103013, #58122 ) ;
#72267=LINE ( 'NONE', #28729, #41892 ) ;
#72268=ORIENTED_EDGE ( 'NONE', *, *, #37292, .F. ) ;
#72269=DIRECTION ( 'NONE',  ( -0.6830127018922181881, 0.6830127018922202975, -0.2588190451025214056 ) ) ;
#72270=VECTOR ( 'NONE', #124132, 1000.000000000000000 ) ;
#72272=FACE_OUTER_BOUND ( 'NONE', #118842, .T. ) ;
#72273=CARTESIAN_POINT ( 'NONE',  ( -5.994519915287488843, 28.92564299267942118, 4.000000000000000000 ) ) ;
#72274=EDGE_LOOP ( 'NONE', ( #98650, #72596, #598, #11884 ) ) ;
#72275=EDGE_CURVE ( 'NONE', #59858, #90775, #125340, .T. ) ;
#72276=CARTESIAN_POINT ( 'NONE',  ( -6.489213562373093325, -27.52281430457059841, 5.000000000000000000 ) ) ;
#72277=DIRECTION ( 'NONE',  ( -0.6830127018922180770, 0.6830127018922202975, -0.2588190451025213501 ) ) ;
#72278=ORIENTED_EDGE ( 'NONE', *, *, #33834, .T. ) ;
#72279=ORIENTED_EDGE ( 'NONE', *, *, #115391, .T. ) ;
#72280=DIRECTION ( 'NONE',  ( -0.7071067811865486830, -0.7071067811865464625, 0.000000000000000000 ) ) ;
#72281=ORIENTED_EDGE ( 'NONE', *, *, #83559, .T. ) ;
#72282=AXIS2_PLACEMENT_3D ( 'NONE', #123524, #100320, #68437 ) ;
#72283=CARTESIAN_POINT ( 'NONE',  ( 5.277185695429377432, -21.72500000000000853, 5.000000000000000000 ) ) ;
#72288=EDGE_LOOP ( 'NONE', ( #46359, #142973, #20455, #31990 ) ) ;
#72289=CARTESIAN_POINT ( 'NONE',  ( -15.48921356237309510, -27.52281430457066236, 5.000000000000000000 ) ) ;
#72290=CARTESIAN_POINT ( 'NONE',  ( -29.99999999999980105, -19.06887692260762179, 4.000000000000000000 ) ) ;
#72292=VECTOR ( 'NONE', #1283, 1000.000000000000000 ) ;
#72293=FACE_OUTER_BOUND ( 'NONE', #102696, .T. ) ;
#72294=LINE ( 'NONE', #94682, #51433 ) ;
#72295=VECTOR ( 'NONE', #21596, 1000.000000000000000 ) ;
#72296=EDGE_LOOP ( 'NONE', ( #17483, #17420, #94275, #116542 ) ) ;
#72298=EDGE_LOOP ( 'NONE', ( #31846, #77428, #28513, #119912 ) ) ;
#72299=EDGE_CURVE ( 'NONE', #56571, #69864, #59396, .T. ) ;
#72301=LINE ( 'NONE', #25887, #36157 ) ;
#72302=LINE ( 'NONE', #38209, #100227 ) ;
#72303=AXIS2_PLACEMENT_3D ( 'NONE', #57418, #113183, #56001 ) ;
#72304=DIRECTION ( 'NONE',  ( -0.7071067811865486830, -0.7071067811865464625, 0.000000000000000000 ) ) ;
#72306=LINE ( 'NONE', #82424, #65126 ) ;
#72307=CARTESIAN_POINT ( 'NONE',  ( -30.18398860626900060, 28.73617430169808173, 5.000000000000000000 ) ) ;
#72308=DIRECTION ( 'NONE',  ( -0.7071067811865486830, -0.7071067811865464625, 0.000000000000000000 ) ) ;
#72309=ADVANCED_FACE ( 'NONE', ( #81868 ), #39034, .F. ) ;
#72310=DIRECTION ( 'NONE',  ( 0.7071067811865486830, -0.7071067811865464625, -0.000000000000000000 ) ) ;
#72311=ORIENTED_EDGE ( 'NONE', *, *, #2924, .F. ) ;
#72312=DIRECTION ( 'NONE',  ( 0.6830127018922180770, -0.6830127018922204085, -0.2588190451025213501 ) ) ;
#72313=CARTESIAN_POINT ( 'NONE',  ( -15.18398860626900237, 28.73617430169797871, 5.000000000000000000 ) ) ;
#72314=AXIS2_PLACEMENT_3D ( 'NONE', #4780, #38202, #5527 ) ;
#72315=DIRECTION ( 'NONE',  ( 0.7071067811865487940, 0.7071067811865463515, 0.000000000000000000 ) ) ;
#72317=ORIENTED_EDGE ( 'NONE', *, *, #97764, .F. ) ;
#72318=ORIENTED_EDGE ( 'NONE', *, *, #70653, .F. ) ;
#72320=ORIENTED_EDGE ( 'NONE', *, *, #20389, .F. ) ;
#72321=DIRECTION ( 'NONE',  ( 0.6830127018922181881, 0.6830127018922202975, -0.2588190451025214056 ) ) ;
#72322=CARTESIAN_POINT ( 'NONE',  ( 23.68342038867195853, -6.740707523384216415, 11.88629033278118641 ) ) ;
#72323=CARTESIAN_POINT ( 'NONE',  ( 13.82816939922343202, 9.759292476615623713, 4.000000000000000000 ) ) ;
#72324=ORIENTED_EDGE ( 'NONE', *, *, #87394, .F. ) ;
#72326=VECTOR ( 'NONE', #119238, 1000.000000000000000 ) ;
#72327=VECTOR ( 'NONE', #128281, 1000.000000000000000 ) ;
#72328=DIRECTION ( 'NONE',  ( 1.000000000000000000, 0.000000000000000000, 0.000000000000000000 ) ) ;
#72329=LINE ( 'NONE', #115030, #69844 ) ;
#72331=ORIENTED_EDGE ( 'NONE', *, *, #33834, .F. ) ;
#72332=LINE ( 'NONE', #127367, #44300 ) ;
#72333=VECTOR ( 'NONE', #112196, 1000.000000000000000 ) ;
#72335=CARTESIAN_POINT ( 'NONE',  ( 72.29974487139158157, -27.71228299555256669, 4.000000000000000000 ) ) ;
#72336=VECTOR ( 'NONE', #6743, 1000.000000000000227 ) ;
#72337=VECTOR ( 'NONE', #59138, 1000.000000000000000 ) ;
#72338=VERTEX_POINT ( 'NONE', #26027 ) ;
#72342=CARTESIAN_POINT ( 'NONE',  ( -5.999999999999954703, -19.22509904557637128, 1.855685503482163767 ) ) ;
#72343=CARTESIAN_POINT ( 'NONE',  ( -31.17183060077625356, 12.75929247661558819, 4.000000000000000000 ) ) ;
#72344=DIRECTION ( 'NONE',  ( -0.7071067811865486830, -0.7071067811865464625, -0.000000000000000000 ) ) ;
#72345=FACE_OUTER_BOUND ( 'NONE', #58257, .T. ) ;
#72346=CARTESIAN_POINT ( 'NONE',  ( -9.851816449618491234, 17.25929247661554200, 8.802941693769181342 ) ) ;
#72347=ORIENTED_EDGE ( 'NONE', *, *, #127110, .F. ) ;
#72348=EDGE_CURVE ( 'NONE', #53474, #53240, #36878, .T. ) ;
#72350=ORIENTED_EDGE ( 'NONE', *, *, #22362, .T. ) ;
#72351=EDGE_CURVE ( 'NONE', #121175, #107840, #58712, .T. ) ;
#72353=EDGE_CURVE ( 'NONE', #46724, #108692, #103554, .T. ) ;
#72354=ADVANCED_FACE ( 'NONE', ( #102879 ), #127466, .F. ) ;
#72355=FACE_OUTER_BOUND ( 'NONE', #114691, .T. ) ;
#72357=DIRECTION ( 'NONE',  ( 0.6830127018922180770, -0.6830127018922204085, -0.2588190451025213501 ) ) ;
#72358=LINE ( 'NONE', #50556, #19382 ) ;
#72359=AXIS2_PLACEMENT_3D ( 'NONE', #17770, #138162, #127263 ) ;
#72360=PLANE ( 'NONE',  #15518 ) ;
#72361=CARTESIAN_POINT ( 'NONE',  ( 34.49999999999975842, 13.56627193232217898, -10.57019076586060713 ) ) ;
#72362=VECTOR ( 'NONE', #106629, 1000.000000000000000 ) ;
#72363=CARTESIAN_POINT ( 'NONE',  ( 26.99999999999981881, -7.447814304570752775, 5.000000000000000000 ) ) ;
#72364=ORIENTED_EDGE ( 'NONE', *, *, #9778, .T. ) ;
#72367=EDGE_CURVE ( 'NONE', #129026, #73447, #48480, .T. ) ;
#72368=EDGE_LOOP ( 'NONE', ( #56694, #34559, #123857, #55128 ) ) ;
#72369=CARTESIAN_POINT ( 'NONE',  ( 31.49999999999978684, 15.05218569542901186, 5.000000000000000000 ) ) ;
#72370=ORIENTED_EDGE ( 'NONE', *, *, #34211, .F. ) ;
#72372=ORIENTED_EDGE ( 'NONE', *, *, #16222, .T. ) ;
#72375=ORIENTED_EDGE ( 'NONE', *, *, #9444, .T. ) ;
#72377=ORIENTED_EDGE ( 'NONE', *, *, #76749, .F. ) ;
#72378=EDGE_CURVE ( 'NONE', #129071, #56327, #113012, .T. ) ;
#72379=DIRECTION ( 'NONE',  ( -0.3543493200069163240, 0.000000000000000000, 0.9351131265310288487 ) ) ;
#72380=DIRECTION ( 'NONE',  ( -4.681814790819591790E-17, -0.3543493200069152693, 0.9351131265310292928 ) ) ;
#72383=AXIS2_PLACEMENT_3D ( 'NONE', #138253, #127362, #72328 ) ;
#72384=CARTESIAN_POINT ( 'NONE',  ( 5.671830600776426756, -21.74070752338406365, 4.000000000000000000 ) ) ;
#72385=LINE ( 'NONE', #128163, #118091 ) ;
#72386=EDGE_CURVE ( 'NONE', #47983, #90340, #71675, .T. ) ;
#72387=PLANE ( 'NONE',  #29067 ) ;
#72388=AXIS2_PLACEMENT_3D ( 'NONE', #12125, #101288, #1927 ) ;
#72389=PLANE ( 'NONE',  #14558 ) ;
#72390=DIRECTION ( 'NONE',  ( -0.7071067811865486830, -0.7071067811865464625, 0.000000000000000000 ) ) ;
#72391=CARTESIAN_POINT ( 'NONE',  ( -9.183988606268997046, 28.73617430169793607, 5.000000000000000000 ) ) ;
#72392=ORIENTED_EDGE ( 'NONE', *, *, #72351, .T. ) ;
#72393=ORIENTED_EDGE ( 'NONE', *, *, #111713, .F. ) ;
#72394=ORIENTED_EDGE ( 'NONE', *, *, #86610, .F. ) ;
#72395=EDGE_CURVE ( 'NONE', #76403, #1315, #92683, .T. ) ;
#72398=ORIENTED_EDGE ( 'NONE', *, *, #130577, .F. ) ;
#72399=CARTESIAN_POINT ( 'NONE',  ( -6.328169399223483538, 2.259292476615696099, 4.000000000000000000 ) ) ;
#72400=DIRECTION ( 'NONE',  ( -0.000000000000000000, 0.000000000000000000, 1.000000000000000000 ) ) ;
#72402=DIRECTION ( 'NONE',  ( 0.7071067811865486830, -0.7071067811865464625, -0.000000000000000000 ) ) ;
#72405=AXIS2_PLACEMENT_3D ( 'NONE', #131998, #89201, #64585 ) ;
#72406=ORIENTED_EDGE ( 'NONE', *, *, #103086, .F. ) ;
#72407=EDGE_CURVE ( 'NONE', #80487, #118264, #126062, .T. ) ;
#72410=CARTESIAN_POINT ( 'NONE',  ( 0.000000000000000000, 21.72500000000000142, 4.500000000000000888 ) ) ;
#72412=VERTEX_POINT ( 'NONE', #136202 ) ;
#72413=ORIENTED_EDGE ( 'NONE', *, *, #102624, .F. ) ;
#72414=ORIENTED_EDGE ( 'NONE', *, *, #101343, .T. ) ;
#72415=LINE ( 'NONE', #105679, #9259 ) ;
#72416=CARTESIAN_POINT ( 'NONE',  ( -2.816011393730999401, 28.73617430169785436, 5.000000000000000000 ) ) ;
#72418=LINE ( 'NONE', #120668, #17262 ) ;
#72419=VECTOR ( 'NONE', #70563, 1000.000000000000000 ) ;
#72420=CARTESIAN_POINT ( 'NONE',  ( -18.48921356237309510, -27.52281430457068367, 5.000000000000000000 ) ) ;
#72422=CARTESIAN_POINT ( 'NONE',  ( 0.000000000000000000, 0.000000000000000000, 5.000000000000000000 ) ) ;
#72424=CARTESIAN_POINT ( 'NONE',  ( 66.48921356237309510, -27.52281430457101763, 5.000000000000000000 ) ) ;
#72425=EDGE_CURVE ( 'NONE', #41011, #141528, #14435, .T. ) ;
#72426=CARTESIAN_POINT ( 'NONE',  ( 21.18398860626899349, 28.73617430169802134, 5.000000000000000000 ) ) ;
#72427=CARTESIAN_POINT ( 'NONE',  ( 24.70710678118637205, -6.740707523384214639, 5.000000000000000000 ) ) ;
#72428=ORIENTED_EDGE ( 'NONE', *, *, #100140, .F. ) ;
#72430=VECTOR ( 'NONE', #131283, 1000.000000000000227 ) ;
#72431=VECTOR ( 'NONE', #121613, 1000.000000000000000 ) ;
#72432=DIRECTION ( 'NONE',  ( 0.7071067811865487940, 0.7071067811865463515, 0.000000000000000000 ) ) ;
#72433=ORIENTED_EDGE ( 'NONE', *, *, #103436, .F. ) ;
#72434=CARTESIAN_POINT ( 'NONE',  ( -19.49999999999985079, 16.08746187583907528, 4.000000000000000000 ) ) ;
#72437=ADVANCED_FACE ( 'NONE', ( #115842 ), #136919, .F. ) ;
#72438=LINE ( 'NONE', #137666, #37615 ) ;
#72440=VERTEX_POINT ( 'NONE', #2827 ) ;
#72443=ORIENTED_EDGE ( 'NONE', *, *, #3721, .F. ) ;
#72444=DIRECTION ( 'NONE',  ( -0.7071067811865486830, -0.7071067811865464625, 0.000000000000000000 ) ) ;
#72446=FACE_OUTER_BOUND ( 'NONE', #126117, .T. ) ;
#72447=VECTOR ( 'NONE', #133734, 1000.000000000000000 ) ;
#72448=DIRECTION ( 'NONE',  ( 0.7071067811865486830, -0.7071067811865464625, -0.000000000000000000 ) ) ;
#72449=LINE ( 'NONE', #6371, #51453 ) ;
#72450=CARTESIAN_POINT ( 'NONE',  ( -1.499999999999982236, -1.912538124160737318, 4.000000000000000000 ) ) ;
#72454=DIRECTION ( 'NONE',  ( 0.7071067811865486830, -0.7071067811865464625, -0.000000000000000000 ) ) ;
#72455=CARTESIAN_POINT ( 'NONE',  ( -9.183988606268997046, 28.73617430169793607, 5.000000000000000000 ) ) ;
#72457=ORIENTED_EDGE ( 'NONE', *, *, #85182, .F. ) ;
#72458=ORIENTED_EDGE ( 'NONE', *, *, #96662, .F. ) ;
#72461=ORIENTED_EDGE ( 'NONE', *, *, #115502, .F. ) ;
#72463=EDGE_CURVE ( 'NONE', #43580, #142125, #93419, .T. ) ;
#72466=CARTESIAN_POINT ( 'NONE',  ( 22.99806943317885199, -22.22500000000000142, 4.500000000000000888 ) ) ;
#72467=VECTOR ( 'NONE', #110392, 1000.000000000000000 ) ;
#72469=CARTESIAN_POINT ( 'NONE',  ( 18.79289321881333308, -11.24070752338417023, 5.000000000000000000 ) ) ;
#72470=ORIENTED_EDGE ( 'NONE', *, *, #93080, .T. ) ;
#72471=CARTESIAN_POINT ( 'NONE',  ( -75.18398860626899705, 28.73617430169839793, 5.000000000000000000 ) ) ;
#72472=LINE ( 'NONE', #116637, #37164 ) ;
#72473=LINE ( 'NONE', #60886, #74170 ) ;
#72474=CARTESIAN_POINT ( 'NONE',  ( 21.29974487139158512, -27.71228299555221142, 4.000000000000000000 ) ) ;
#72475=EDGE_CURVE ( 'NONE', #13343, #103863, #5665, .T. ) ;
#72476=EDGE_CURVE ( 'NONE', #88862, #22212, #135513, .T. ) ;
#72477=CARTESIAN_POINT ( 'NONE',  ( -5.816011393731002066, 28.73617430169783304, 5.000000000000000000 ) ) ;
#72478=CARTESIAN_POINT ( 'NONE',  ( 17.99451991528748351, 28.92564299267950645, 4.000000000000000000 ) ) ;
#72479=DIRECTION ( 'NONE',  ( 0.6830127018922180770, -0.6830127018922204085, -0.2588190451025213501 ) ) ;
#72480=CARTESIAN_POINT ( 'NONE',  ( -19.62823445044373116, -8.240707523384196875, 11.38925528200757142 ) ) ;
#72481=LINE ( 'NONE', #48545, #112778 ) ;
#72482=DIRECTION ( 'NONE',  ( -0.7071067811865486830, -0.7071067811865464625, 0.000000000000000000 ) ) ;
#72483=CARTESIAN_POINT ( 'NONE',  ( 4.499999999999972466, -2.173586137069131841, -4.605770156576102003 ) ) ;
#72484=VECTOR ( 'NONE', #89846, 1000.000000000000227 ) ;
#72485=ORIENTED_EDGE ( 'NONE', *, *, #115359, .F. ) ;
#72486=ORIENTED_EDGE ( 'NONE', *, *, #102732, .T. ) ;
#72488=ORIENTED_EDGE ( 'NONE', *, *, #79145, .F. ) ;
#72489=VECTOR ( 'NONE', #124179, 1000.000000000000000 ) ;
#72490=FACE_OUTER_BOUND ( 'NONE', #65067, .T. ) ;
#72491=VECTOR ( 'NONE', #46443, 1000.000000000000227 ) ;
#72492=DIRECTION ( 'NONE',  ( -0.3543493200069162685, -0.000000000000000000, -0.9351131265310288487 ) ) ;
#72494=EDGE_CURVE ( 'NONE', #79059, #132154, #86834, .T. ) ;
#72495=PLANE ( 'NONE',  #7425 ) ;
#72497=( BOUNDED_CURVE ( )  B_SPLINE_CURVE ( 3, ( #10548, #384, #57677, #134509 ),
 .UNSPECIFIED., .F., .F. ) 
 B_SPLINE_CURVE_WITH_KNOTS ( ( 4, 4 ),
 ( 5.005968288816720069, 5.074607125596358514 ),
 .UNSPECIFIED. ) 
 CURVE ( )  GEOMETRIC_REPRESENTATION_ITEM ( )  RATIONAL_B_SPLINE_CURVE ( ( 1.000000000000000000, 0.9996074310407762065, 0.9996074310407762065, 1.000000000000000000 ) ) 
 REPRESENTATION_ITEM ( '' )  );
#72500=DIRECTION ( 'NONE',  ( -0.7071067811865486830, -0.7071067811865464625, 0.000000000000000000 ) ) ;
#72502=CARTESIAN_POINT ( 'NONE',  ( 8.241399257801971245, 21.72500000000000142, 5.000000000000000000 ) ) ;
#72503=VECTOR ( 'NONE', #109187, 1000.000000000000000 ) ;
#72504=CARTESIAN_POINT ( 'NONE',  ( 22.49999999999984723, 15.05218569542901541, 5.000000000000000000 ) ) ;
#72505=CARTESIAN_POINT ( 'NONE',  ( -45.29974487139158867, -27.71228299555237840, 4.000000000000000000 ) ) ;
#72506=( BOUNDED_CURVE ( )  B_SPLINE_CURVE ( 3, ( #1924, #2669, #102006, #34610 ),
 .UNSPECIFIED., .F., .T. ) 
 B_SPLINE_CURVE_WITH_KNOTS ( ( 4, 4 ),
 ( 2.280733380739273564, 2.329266631601944137 ),
 .UNSPECIFIED. ) 
 CURVE ( )  GEOMETRIC_REPRESENTATION_ITEM ( )  RATIONAL_B_SPLINE_CURVE ( ( 1.000000000000000000, 0.9998037199289477872, 0.9998037199289477872, 1.000000000000000000 ) ) 
 REPRESENTATION_ITEM ( '' )  );
#72507=LINE ( 'NONE', #113273, #22996 ) ;
#72508=VERTEX_POINT ( 'NONE', #61540 ) ;
#72509=ORIENTED_EDGE ( 'NONE', *, *, #83795, .T. ) ;
#72510=ORIENTED_EDGE ( 'NONE', *, *, #116834, .F. ) ;
#72511=CARTESIAN_POINT ( 'NONE',  ( -24.70057660522904897, 5.105512181938189009, 4.576947331497495774 ) ) ;
#72512=CARTESIAN_POINT ( 'NONE',  ( 66.48921356237309510, -27.52281430457101763, 5.000000000000000000 ) ) ;
#72514=VECTOR ( 'NONE', #89043, 1000.000000000000000 ) ;
#72515=LINE ( 'NONE', #19503, #1586 ) ;
#72516=ADVANCED_FACE ( 'NONE', ( #74541 ), #118725, .T. ) ;
#72518=ORIENTED_EDGE ( 'NONE', *, *, #26560, .F. ) ;
#72519=EDGE_CURVE ( 'NONE', #71568, #8795, #119419, .T. ) ;
#72520=PLANE ( 'NONE',  #66529 ) ;
#72521=EDGE_LOOP ( 'NONE', ( #100034, #114181, #40273, #28352 ) ) ;
#72522=VERTEX_POINT ( 'NONE', #28164 ) ;
#72523=VECTOR ( 'NONE', #31205, 999.9999999999998863 ) ;
#72524=EDGE_CURVE ( 'NONE', #81146, #63415, #39778, .T. ) ;
#72526=EDGE_CURVE ( 'NONE', #43949, #87685, #96939, .T. ) ;
#72528=VECTOR ( 'NONE', #115428, 1000.000000000000000 ) ;
#72529=DIRECTION ( 'NONE',  ( -0.7071067811865487940, 0.7071067811865463515, -0.000000000000000000 ) ) ;
#72530=DIRECTION ( 'NONE',  ( -0.6830127018922180770, -0.6830127018922204085, -0.2588190451025213501 ) ) ;
#72531=ORIENTED_EDGE ( 'NONE', *, *, #118737, .F. ) ;
#72532=DIRECTION ( 'NONE',  ( 0.7071067811865487940, 0.7071067811865463515, 0.000000000000000000 ) ) ;
#72534=CARTESIAN_POINT ( 'NONE',  ( 2.510786437626908008, -27.52281430457053446, 5.000000000000000000 ) ) ;
#72536=DIRECTION ( 'NONE',  ( -0.000000000000000000, 0.000000000000000000, 1.000000000000000000 ) ) ;
#72537=CARTESIAN_POINT ( 'NONE',  ( 30.66846741159838530, -18.74070752338408852, 20.73178291233848469 ) ) ;
#72538=EDGE_LOOP ( 'NONE', ( #79805, #140185, #53974, #120623 ) ) ;
#72539=LINE ( 'NONE', #125449, #39500 ) ;
#72541=ADVANCED_FACE ( 'NONE', ( #41167 ), #105687, .F. ) ;
#72542=ORIENTED_EDGE ( 'NONE', *, *, #47458, .F. ) ;
#72544=CARTESIAN_POINT ( 'NONE',  ( 27.06011071044003202, -9.740707523384184441, 10.89222023123374505 ) ) ;
#72547=ORIENTED_EDGE ( 'NONE', *, *, #53533, .T. ) ;
#72548=CARTESIAN_POINT ( 'NONE',  ( -12.29974487139158512, -27.71228299555214747, 4.000000000000000000 ) ) ;
#72549=VERTEX_POINT ( 'NONE', #62234 ) ;
#72550=ORIENTED_EDGE ( 'NONE', *, *, #62155, .F. ) ;
#72553=ORIENTED_EDGE ( 'NONE', *, *, #88229, .F. ) ;
#72554=AXIS2_PLACEMENT_3D ( 'NONE', #89331, #21924, #45853 ) ;
#72555=EDGE_CURVE ( 'NONE', #63684, #140803, #19419, .T. ) ;
#72558=CARTESIAN_POINT ( 'NONE',  ( -34.47516574401891631, -2.971932658884152367, 4.998110765256834398 ) ) ;
#72559=CARTESIAN_POINT ( 'NONE',  ( -18.29974487139159223, -27.71228299555219010, 4.000000000000000000 ) ) ;
#72560=DIRECTION ( 'NONE',  ( -0.6830127018922180770, -0.6830127018922204085, -0.2588190451025213501 ) ) ;
#72561=CARTESIAN_POINT ( 'NONE',  ( -69.48921356237309510, -27.52281430457103895, 5.000000000000000000 ) ) ;
#72562=EDGE_CURVE ( 'NONE', #6240, #82809, #140368, .T. ) ;
#72563=VECTOR ( 'NONE', #90346, 1000.000000000000000 ) ;
#72564=CARTESIAN_POINT ( 'NONE',  ( -45.29974487139158867, -27.71228299555237840, 4.000000000000000000 ) ) ;
#72565=LINE ( 'NONE', #82001, #99202 ) ;
#72566=DIRECTION ( 'NONE',  ( -0.3543493200069162685, -0.000000000000000000, -0.9351131265310288487 ) ) ;
#72567=AXIS2_PLACEMENT_3D ( 'NONE', #39392, #126373, #83624 ) ;
#72568=CARTESIAN_POINT ( 'NONE',  ( 0.4892135623730947680, -27.52281430457055578, 5.000000000000000000 ) ) ;
#72569=ORIENTED_EDGE ( 'NONE', *, *, #54184, .F. ) ;
#72570=ORIENTED_EDGE ( 'NONE', *, *, #111778, .T. ) ;
#72571=ADVANCED_FACE ( 'NONE', ( #8497 ), #107135, .F. ) ;
#72572=ORIENTED_EDGE ( 'NONE', *, *, #53098, .T. ) ;
#72573=ORIENTED_EDGE ( 'NONE', *, *, #10159, .F. ) ;
#72576=VECTOR ( 'NONE', #69345, 1000.000000000000000 ) ;
#72577=ORIENTED_EDGE ( 'NONE', *, *, #65335, .F. ) ;
#72578=CARTESIAN_POINT ( 'NONE',  ( 26.99451991528749417, 28.92564299267956685, 4.000000000000000000 ) ) ;
#72580=EDGE_CURVE ( 'NONE', #117925, #13143, #31033, .T. ) ;
#72582=EDGE_CURVE ( 'NONE', #38491, #77870, #67974, .T. ) ;
#72583=CARTESIAN_POINT ( 'NONE',  ( 21.71715331601274102, -2.164967620583693630, 5.000000000000000000 ) ) ;
#72584=ORIENTED_EDGE ( 'NONE', *, *, #28800, .F. ) ;
#72585=CARTESIAN_POINT ( 'NONE',  ( -5.999999999999956479, -6.108550654416966097, -3.114665004254979941 ) ) ;
#72586=VECTOR ( 'NONE', #15564, 1000.000000000000000 ) ;
#72587=EDGE_CURVE ( 'NONE', #32455, #75311, #143338, .T. ) ;
#72589=AXIS2_PLACEMENT_3D ( 'NONE', #28706, #4726, #72243 ) ;
#72591=ORIENTED_EDGE ( 'NONE', *, *, #36713, .T. ) ;
#72593=FACE_OUTER_BOUND ( 'NONE', #46804, .T. ) ;
#72595=DIRECTION ( 'NONE',  ( 0.6830127018922181881, 0.6830127018922202975, -0.2588190451025214056 ) ) ;
#72596=ORIENTED_EDGE ( 'NONE', *, *, #48156, .T. ) ;
#72597=VERTEX_POINT ( 'NONE', #21572 ) ;
#72598=ORIENTED_EDGE ( 'NONE', *, *, #86707, .F. ) ;
#72600=AXIS2_PLACEMENT_3D ( 'NONE', #99622, #90933, #11160 ) ;
#72601=LINE ( 'NONE', #118894, #32537 ) ;
#72602=CARTESIAN_POINT ( 'NONE',  ( -17.51078643762690845, -27.52281430457043143, 5.000000000000000000 ) ) ;
#72603=EDGE_LOOP ( 'NONE', ( #88433, #107694, #49151, #73388 ) ) ;
#72604=LINE ( 'NONE', #81308, #78397 ) ;
#72605=DIRECTION ( 'NONE',  ( 0.7071067811865487940, 0.7071067811865463515, 0.000000000000000000 ) ) ;
#72606=DIRECTION ( 'NONE',  ( -0.000000000000000000, -0.3543493200069152693, 0.9351131265310292928 ) ) ;
#72607=ORIENTED_EDGE ( 'NONE', *, *, #3823, .F. ) ;
#72608=DIRECTION ( 'NONE',  ( 0.7071067811865487940, 0.7071067811865463515, 0.000000000000000000 ) ) ;
#72609=VECTOR ( 'NONE', #14220, 1000.000000000000000 ) ;
#72610=LINE ( 'NONE', #129066, #42500 ) ;
#72611=ORIENTED_EDGE ( 'NONE', *, *, #30142, .F. ) ;
#72612=DIRECTION ( 'NONE',  ( 0.7071067811865487940, -0.7071067811865463515, 0.000000000000000000 ) ) ;
#72613=EDGE_LOOP ( 'NONE', ( #91496, #91970, #137815, #24477, #37439, #15542, #140428, #82744, #98829, #103726, #28938, #127828, #50703, #93394, #98748, #5768, #61138, #84119, #140034, #66672, #38794, #90584, #55638, #35642, #40840, #138011, #62668, #66079, #122174, #67619, #39570, #3976, #108341, #51077, #123764, #24008, #4296, #119714, #62885, #73417, #112170, #131466, #116999, #133301, #48987, #17656, #9735, #141501, #130854, #55042, #35781, #138112, #68261, #36232, #105890, #111404, #17663, #28969, #87096, #126259, #60113, #65701, #97276, #99669, #135307, #61760, #98723, #32485, #125865, #10335, #73605, #14398, #89827, #2091, #4866, #26914, #113579, #69512, #23015, #416, #89885, #1822, #53502, #87293, #28324, #24643, #56774, #124929, #98028, #36571, #103474, #102720, #133655, #89512, #127207, #24818, #97887, #125590, #29015, #35296, #104974, #126291, #27011, #50724, #45002, #55591, #140775, #142223, #105419, #76189, #68088, #35348, #86690, #123897, #108361, #26030, #37848, #30570, #119794, #138719, #51128, #31885, #136961, #104488, #69550, #11359, #31127, #83323, #134824, #55006, #27541, #29510, #130106, #11255, #85691, #83735, #54441, #131327, #42896, #2156, #126615, #48754, #96741, #35289, #97741, #22131, #127267, #47202, #94254, #100898, #58419, #79913, #89573, #59267, #6956, #72856, #84453, #61869, #103686, #7922, #23032, #115075, #96851, #85805, #88317, #140978, #117616, #81461, #18864, #4329, #34317, #5285, #117414, #18689, #57515, #122582, #27635, #92808, #93676, #99171, #32948, #33694, #88994, #41338, #139964, #25229, #95393, #87519, #138078, #1962, #140573, #66159, #57542, #14856, #104242, #95823, #109271, #1728, #142419, #134601, #26804, #128622, #115115, #63872, #59758, #32622, #96520, #41703, #92854, #91468, #119320, #68116, #7877, #91057, #53415, #59145, #70796, #28692, #80207, #1444, #81809, #30813, #117079, #99459, #108626, #19321, #110284, #118419, #8421, #42887, #136350, #134727, #36423, #120539, #137984, #117209, #65111, #88959, #23328, #50036, #79024, #23953, #5529, #90154, #5967, #125003, #65013, #57478, #64648, #38467, #61332, #118544, #12823, #98607, #98470, #65373, #84997, #17668, #71011, #136462, #30620, #53956, #132110, #62328, #82735, #36129, #78243, #41672, #52964, #103952, #20423, #97337, #123310, #67922, #128926, #65754, #87227, #54267, #109205, #13609, #122968, #105290, #84152, #131039, #79682, #127699, #139483, #106014, #7926, #30128, #36188, #105454, #138915, #91492, #93911, #71536, #1759, #75012, #116448, #40392, #73681, #104391, #3815, #48035, #110925, #7528, #141697, #72485, #135755, #60557, #121295, #139851, #1495, #115606, #57490, #92563, #16951, #76126, #48131, #124924, #129486, #120432, #78308, #6443, #92175, #138631, #80219, #44681, #78619, #2160, #107833, #135737, #104603, #130488, #87718, #141382, #92865, #93043, #106192, #11029, #119387, #134811, #77984, #104446, #63776, #32399, #5578, #46368, #132530, #69743, #47074, #92846, #64423, #83207, #99563, #41378, #66666, #127345, #107372, #115136, #127556, #57856, #140334, #131316, #11792, #113127, #11505, #34338, #18, #92576, #36165, #65398, #27817, #43134, #77469, #13779, #104701, #120843, #65805, #115459, #15044, #47552, #142434, #87276, #48731, #77136, #7448, #110798, #33719, #55032, #16324, #62222, #45201, #66662, #55805, #78341, #134954, #74076, #73972, #72638, #96947, #75851, #63492, #80181, #31808, #78091, #7161, #64269, #83772, #139980, #86053, #140448, #8444, #70436, #80157, #7079, #96, #83701, #121802, #114026, #57381, #25156, #116398, #86587, #12635, #39136, #56929, #109887, #107538, #133923, #25355, #21560, #94145, #59693, #9979, #47680, #105985, #121687, #112949, #89092, #42305, #124561, #91407, #760, #24691, #114119, #75399, #17736, #140116, #21108, #44895, #46169, #110143, #54773, #37014, #138174, #20928, #11022, #133241, #45165, #89463, #39112, #97572, #28377, #27614, #125729, #33691, #93854, #74082, #93922, #127091, #84658, #114648, #19203, #100223, #6717, #82534, #117923, #1555, #91701, #23273, #36457, #47577, #130267, #56528, #104838, #34803, #51187, #92109, #141107, #990, #23605, #67547, #133534, #39781, #142316, #113820, #45588, #69414, #68746, #51060, #106573, #106000, #88937, #51320, #84256, #128548, #143043, #5571, #107277, #92772, #85518, #88386, #41767, #110835, #45904, #68237, #84238, #120427, #36975, #50184, #83788, #88019, #41241, #10665, #65633, #41329, #95149, #25264, #52452, #62864, #129634, #53336, #100310, #140614, #92876, #8406, #54326, #40765, #35199, #8324, #76482, #131982, #9886, #73246, #111381, #57139, #14475, #121630, #84635, #39789, #111215, #43667, #74421, #40772, #45969, #56371, #124180, #35218, #139897, #5923, #71886, #93525, #82689, #40541, #103074, #102883, #40596, #76161, #130485, #28620, #73796, #102981, #2115, #80694, #41837, #133627, #11661, #20357, #18240, #53472, #4044, #10592, #59898, #111421, #60132, #24241, #103030, #103079, #62545, #42730, #57940, #89179, #96563, #32521, #4370, #17087, #132044, #136640, #63436, #70272, #57023, #95442, #67341 ) ) ;
#72615=VECTOR ( 'NONE', #113434, 1000.000000000000000 ) ;
#72616=DIRECTION ( 'NONE',  ( 0.7071067811865487940, 0.7071067811865463515, -0.000000000000000000 ) ) ;
#72617=ORIENTED_EDGE ( 'NONE', *, *, #15752, .T. ) ;
#72618=DIRECTION ( 'NONE',  ( 0.7071067811865487940, 0.7071067811865463515, 0.000000000000000000 ) ) ;
#72619=CARTESIAN_POINT ( 'NONE',  ( -53.99451991528749062, 28.92564299267975869, 4.000000000000000000 ) ) ;
#72621=VECTOR ( 'NONE', #4880, 1000.000000000000000 ) ;
#72622=VERTEX_POINT ( 'NONE', #44040 ) ;
#72623=PLANE ( 'NONE',  #36932 ) ;
#72624=LINE ( 'NONE', #137122, #28045 ) ;
#72625=EDGE_CURVE ( 'NONE', #102057, #78692, #22246, .T. ) ;
#72626=CARTESIAN_POINT ( 'NONE',  ( -0.7928932188134502068, -20.24070752338407431, 5.000000000000000000 ) ) ;
#72627=CARTESIAN_POINT ( 'NONE',  ( -42.18398860626899705, 28.73617430169816700, 5.000000000000000000 ) ) ;
#72628=FACE_OUTER_BOUND ( 'NONE', #18803, .T. ) ;
#72629=CARTESIAN_POINT ( 'NONE',  ( 32.99999999999977973, 8.966399257802176948, 5.000000000000000000 ) ) ;
#72631=CARTESIAN_POINT ( 'NONE',  ( -1.828169399223505964, 3.759292476615685441, 4.000000000000000000 ) ) ;
#72632=DIRECTION ( 'NONE',  ( -0.6830127018922180770, -0.6830127018922204085, -0.2588190451025213501 ) ) ;
#72633=EDGE_LOOP ( 'NONE', ( #14556, #138661, #135169, #98459 ) ) ;
#72634=VECTOR ( 'NONE', #15243, 1000.000000000000000 ) ;
#72636=ORIENTED_EDGE ( 'NONE', *, *, #115097, .F. ) ;
#72638=ORIENTED_EDGE ( 'NONE', *, *, #20245, .F. ) ;
#72639=ORIENTED_EDGE ( 'NONE', *, *, #7742, .F. ) ;
#72640=VERTEX_POINT ( 'NONE', #57080 ) ;
#72642=DIRECTION ( 'NONE',  ( -0.7071067811865486830, 0.7071067811865463515, 0.000000000000000000 ) ) ;
#72643=DIRECTION ( 'NONE',  ( -0.7071067811865486830, 0.7071067811865464625, 0.000000000000000000 ) ) ;
#72644=ORIENTED_EDGE ( 'NONE', *, *, #18793, .F. ) ;
#72645=DIRECTION ( 'NONE',  ( -0.7071067811865487940, 0.7071067811865463515, -0.000000000000000000 ) ) ;
#72646=LINE ( 'NONE', #140690, #90344 ) ;
#72647=DIRECTION ( 'NONE',  ( -0.7071067811865487940, 0.7071067811865463515, 0.000000000000000000 ) ) ;
#72648=CARTESIAN_POINT ( 'NONE',  ( -18.48921356237309510, -27.52281430457068367, 5.000000000000000000 ) ) ;
#72650=EDGE_CURVE ( 'NONE', #5966, #11091, #12100, .T. ) ;
#72655=EDGE_CURVE ( 'NONE', #14518, #63299, #133899, .T. ) ;
#72656=CARTESIAN_POINT ( 'NONE',  ( -23.99451991528749062, 28.92564299267954908, 4.000000000000000000 ) ) ;
#72657=LINE ( 'NONE', #40011, #9659 ) ;
#72658=VECTOR ( 'NONE', #142918, 1000.000000000000227 ) ;
#72659=EDGE_CURVE ( 'NONE', #51451, #71767, #88262, .T. ) ;
#72660=DIRECTION ( 'NONE',  ( 0.6830127018922180770, -0.6830127018922204085, -0.2588190451025213501 ) ) ;
#72665=DIRECTION ( 'NONE',  ( -0.7071067811865486830, -0.7071067811865464625, 0.000000000000000000 ) ) ;
#72667=ORIENTED_EDGE ( 'NONE', *, *, #61545, .F. ) ;
#72669=VERTEX_POINT ( 'NONE', #55634 ) ;
#72670=ADVANCED_FACE ( 'NONE', ( #45494 ), #132512, .F. ) ;
#72671=CARTESIAN_POINT ( 'NONE',  ( -34.92500000000001137, -22.22500000000000142, 4.000000000000000000 ) ) ;
#72672=CARTESIAN_POINT ( 'NONE',  ( 69.48921356237309510, -27.52281430457103895, 5.000000000000000000 ) ) ;
#72673=CARTESIAN_POINT ( 'NONE',  ( -1.171830600776451625, 12.75929247661558996, 4.000000000000000000 ) ) ;
#72674=VECTOR ( 'NONE', #32801, 1000.000000000000000 ) ;
#72675=LINE ( 'NONE', #117521, #7477 ) ;
#72676=EDGE_CURVE ( 'NONE', #121862, #121313, #33197, .T. ) ;
#72678=CARTESIAN_POINT ( 'NONE',  ( 22.17183060077631751, -20.24070752338407431, 4.000000000000000000 ) ) ;
#72680=VECTOR ( 'NONE', #60271, 1000.000000000000000 ) ;
#72681=ORIENTED_EDGE ( 'NONE', *, *, #83785, .T. ) ;
#72682=DIRECTION ( 'NONE',  ( -0.7071067811865487940, 0.7071067811865463515, 0.000000000000000000 ) ) ;
#72683=ORIENTED_EDGE ( 'NONE', *, *, #114850, .T. ) ;
#72684=DIRECTION ( 'NONE',  ( -0.6830127018922181881, 0.6830127018922202975, -0.2588190451025214056 ) ) ;
#72685=ADVANCED_FACE ( 'NONE', ( #34590 ), #65830, .F. ) ;
#72686=PLANE ( 'NONE',  #49989 ) ;
#72688=DIRECTION ( 'NONE',  ( 1.000000000000000000, 0.000000000000000000, 0.000000000000000000 ) ) ;
#72689=ORIENTED_EDGE ( 'NONE', *, *, #66779, .F. ) ;
#72693=DIRECTION ( 'NONE',  ( 0.6830127018922181881, 0.6830127018922202975, -0.2588190451025214056 ) ) ;
#72694=CARTESIAN_POINT ( 'NONE',  ( -25.82816939922335209, -2.240707523384255939, 4.000000000000000000 ) ) ;
#72695=EDGE_CURVE ( 'NONE', #112409, #63022, #43327, .T. ) ;
#72696=CARTESIAN_POINT ( 'NONE',  ( -26.67183060077628198, 20.25929247661550647, 4.000000000000000000 ) ) ;
#72697=( BOUNDED_CURVE ( )  B_SPLINE_CURVE ( 3, ( #54609, #120522, #137508, #129466 ),
 .UNSPECIFIED., .F., .T. ) 
 B_SPLINE_CURVE_WITH_KNOTS ( ( 4, 4 ),
 ( 2.099584536334365925, 2.152415457235772323 ),
 .UNSPECIFIED. ) 
 CURVE ( )  GEOMETRIC_REPRESENTATION_ITEM ( )  RATIONAL_B_SPLINE_CURVE ( ( 1.000000000000000000, 0.9997674213408587196, 0.9997674213408587196, 1.000000000000000000 ) ) 
 REPRESENTATION_ITEM ( '' )  );
#72699=VECTOR ( 'NONE', #66649, 999.9999999999998863 ) ;
#72702=LINE ( 'NONE', #82132, #51182 ) ;
#72703=EDGE_CURVE ( 'NONE', #33545, #138262, #11357, .T. ) ;
#72704=LINE ( 'NONE', #108092, #59507 ) ;
#72705=VERTEX_POINT ( 'NONE', #131046 ) ;
#72706=ORIENTED_EDGE ( 'NONE', *, *, #56068, .T. ) ;
#72707=VECTOR ( 'NONE', #41022, 1000.000000000000000 ) ;
#72708=DIRECTION ( 'NONE',  ( -0.000000000000000000, -1.000000000000000000, -0.000000000000000000 ) ) ;
#72709=ORIENTED_EDGE ( 'NONE', *, *, #74468, .F. ) ;
#72710=EDGE_CURVE ( 'NONE', #22968, #103695, #501, .T. ) ;
#72711=EDGE_CURVE ( 'NONE', #94963, #136607, #120861, .T. ) ;
#72713=ORIENTED_EDGE ( 'NONE', *, *, #114830, .T. ) ;
#72714=CARTESIAN_POINT ( 'NONE',  ( 17.82446237275610201, 9.017796866808286183, 4.672399651904014739 ) ) ;
#72715=DIRECTION ( 'NONE',  ( -0.3543493200069162685, -0.000000000000000000, -0.9351131265310288487 ) ) ;
#72717=EDGE_CURVE ( 'NONE', #47692, #26872, #75948, .T. ) ;
#72718=CARTESIAN_POINT ( 'NONE',  ( -47.99451991528749062, 28.92564299267971251, 4.000000000000000000 ) ) ;
#72719=FACE_BOUND ( 'NONE', #59221, .T. ) ;
#72720=ADVANCED_FACE ( 'NONE', ( #32450 ), #76690, .T. ) ;
#72722=CARTESIAN_POINT ( 'NONE',  ( 0.000000000000000000, 0.000000000000000000, 5.000000000000000000 ) ) ;
#72723=CARTESIAN_POINT ( 'NONE',  ( 9.489213562373095101, -27.52281430457062328, 5.000000000000000000 ) ) ;
#72724=EDGE_CURVE ( 'NONE', #96482, #59299, #70951, .T. ) ;
#72725=VERTEX_POINT ( 'NONE', #22950 ) ;
#72727=CARTESIAN_POINT ( 'NONE',  ( 72.18398860626899705, 28.73617430169837661, 5.000000000000000000 ) ) ;
#72728=VERTEX_POINT ( 'NONE', #15636 ) ;
#72730=LINE ( 'NONE', #84294, #79592 ) ;
#72731=ORIENTED_EDGE ( 'NONE', *, *, #68310, .F. ) ;
#72733=VECTOR ( 'NONE', #111571, 1000.000000000000000 ) ;
#72734=VERTEX_POINT ( 'NONE', #37456 ) ;
#72735=EDGE_CURVE ( 'NONE', #34241, #43058, #4749, .T. ) ;
#72736=PLANE ( 'NONE',  #76594 ) ;
#72737=CARTESIAN_POINT ( 'NONE',  ( -25.82816939922335209, 0.7592924766157138627, 4.000000000000000000 ) ) ;
#72739=LINE ( 'NONE', #95851, #120844 ) ;
#72740=EDGE_CURVE ( 'NONE', #33461, #31488, #101981, .T. ) ;
#72741=VECTOR ( 'NONE', #116527, 1000.000000000000000 ) ;
#72742=DIRECTION ( 'NONE',  ( 0.7071067811865487940, -0.7071067811865463515, 0.000000000000000000 ) ) ;
#72743=LINE ( 'NONE', #6658, #117670 ) ;
#72744=DIRECTION ( 'NONE',  ( 0.7071067811865486830, -0.7071067811865464625, -0.000000000000000000 ) ) ;
#72745=CARTESIAN_POINT ( 'NONE',  ( -56.99451991528749062, 28.92564299267978001, 4.000000000000000000 ) ) ;
#72746=FACE_OUTER_BOUND ( 'NONE', #43727, .T. ) ;
#72747=ORIENTED_EDGE ( 'NONE', *, *, #143188, .T. ) ;
#72748=ORIENTED_EDGE ( 'NONE', *, *, #56255, .T. ) ;
#72749=DIRECTION ( 'NONE',  ( -0.000000000000000000, 0.3543493200069153248, 0.9351131265310292928 ) ) ;
#72750=LINE ( 'NONE', #5965, #106822 ) ;
#72751=EDGE_LOOP ( 'NONE', ( #135553, #1513, #28199, #85607 ) ) ;
#72753=ORIENTED_EDGE ( 'NONE', *, *, #119876, .T. ) ;
#72754=CARTESIAN_POINT ( 'NONE',  ( 17.99999999999987210, -21.84840872380823029, 2.849755605029649974 ) ) ;
#72755=DIRECTION ( 'NONE',  ( 0.6830127018922180770, -0.6830127018922204085, -0.2588190451025213501 ) ) ;
#72756=ORIENTED_EDGE ( 'NONE', *, *, #70375, .T. ) ;
#72757=CARTESIAN_POINT ( 'NONE',  ( -3.489213562373097322, -27.52281430457057709, 5.000000000000000000 ) ) ;
#72758=VECTOR ( 'NONE', #96027, 1000.000000000000000 ) ;
#72759=ADVANCED_FACE ( 'NONE', ( #16366 ), #80258, .F. ) ;
#72761=EDGE_CURVE ( 'NONE', #133481, #116655, #71508, .T. ) ;
#72762=VECTOR ( 'NONE', #36742, 1000.000000000000000 ) ;
#72764=DIRECTION ( 'NONE',  ( 1.000000000000000000, 0.000000000000000000, 0.000000000000000000 ) ) ;
#72766=DIRECTION ( 'NONE',  ( 0.7071067811865487940, -0.7071067811865463515, 0.000000000000000000 ) ) ;
#72767=CARTESIAN_POINT ( 'NONE',  ( 26.99999999999980460, -10.06887692260771772, 4.000000000000000000 ) ) ;
#72768=DIRECTION ( 'NONE',  ( 1.000000000000000000, 0.000000000000000000, 0.000000000000000000 ) ) ;
#72769=PLANE ( 'NONE',  #33332 ) ;
#72770=ORIENTED_EDGE ( 'NONE', *, *, #108662, .F. ) ;
#72772=VERTEX_POINT ( 'NONE', #48315 ) ;
#72773=CARTESIAN_POINT ( 'NONE',  ( 44.99451991528749772, 28.92564299267969474, 4.000000000000000000 ) ) ;
#72774=CARTESIAN_POINT ( 'NONE',  ( -31.49999999999977263, -14.70932175296478128, -11.46312253303829287 ) ) ;
#72775=DIRECTION ( 'NONE',  ( 0.7071067811865487940, -0.7071067811865463515, 0.000000000000000000 ) ) ;
#72777=PLANE ( 'NONE',  #50320 ) ;
#72778=VECTOR ( 'NONE', #128197, 1000.000000000000000 ) ;
#72779=CARTESIAN_POINT ( 'NONE',  ( -32.99999999999976552, -4.068876922607779001, 4.000000000000000000 ) ) ;
#72780=PLANE ( 'NONE',  #127547 ) ;
#72781=PLANE ( 'NONE',  #106900 ) ;
#72782=ORIENTED_EDGE ( 'NONE', *, *, #82850, .T. ) ;
#72783=DIRECTION ( 'NONE',  ( 0.6830127018922181881, 0.6830127018922202975, -0.2588190451025214056 ) ) ;
#72784=DIRECTION ( 'NONE',  ( 0.7071067811865486830, -0.7071067811865464625, -0.000000000000000000 ) ) ;
#72785=CARTESIAN_POINT ( 'NONE',  ( -27.18398860626900060, 28.73617430169806042, 5.000000000000000000 ) ) ;
#72786=VECTOR ( 'NONE', #141572, 1000.000000000000000 ) ;
#72787=DIRECTION ( 'NONE',  ( -0.7071067811865486830, -0.7071067811865464625, 0.000000000000000000 ) ) ;
#72789=AXIS2_PLACEMENT_3D ( 'NONE', #5819, #15265, #81299 ) ;
#72790=ORIENTED_EDGE ( 'NONE', *, *, #136838, .T. ) ;
#72791=ORIENTED_EDGE ( 'NONE', *, *, #30216, .F. ) ;
#72792=CARTESIAN_POINT ( 'NONE',  ( 18.18398860626898994, 28.73617430169800002, 5.000000000000000000 ) ) ;
#72793=VECTOR ( 'NONE', #136156, 1000.000000000000000 ) ;
#72795=DIRECTION ( 'NONE',  ( -0.3543493200069162685, -0.000000000000000000, -0.9351131265310288487 ) ) ;
#72796=VECTOR ( 'NONE', #22052, 1000.000000000000000 ) ;
#72797=DIRECTION ( 'NONE',  ( -0.000000000000000000, 0.3543493200069153248, 0.9351131265310291818 ) ) ;
#72798=CARTESIAN_POINT ( 'NONE',  ( -1.499999999999989120, 0.4311230773921797543, 4.000000000000000000 ) ) ;
#72799=LINE ( 'NONE', #85744, #76860 ) ;
#72800=ORIENTED_EDGE ( 'NONE', *, *, #19603, .T. ) ;
#72801=DIRECTION ( 'NONE',  ( -0.7071067811865486830, 0.7071067811865464625, 0.000000000000000000 ) ) ;
#72802=EDGE_CURVE ( 'NONE', #26788, #62844, #2647, .T. ) ;
#72803=CARTESIAN_POINT ( 'NONE',  ( 34.49999999999975131, -5.945670655168991736, 4.994342998332164996 ) ) ;
#72804=CARTESIAN_POINT ( 'NONE',  ( -1.499999999999992673, -15.29013452822854902, 0.3645803511610323233 ) ) ;
#72805=CARTESIAN_POINT ( 'NONE',  ( 18.48921356237309510, -27.52281430457068367, 5.000000000000000000 ) ) ;
#72807=CARTESIAN_POINT ( 'NONE',  ( -21.75860074219781382, 21.72500000000000142, 5.000000000000000000 ) ) ;
#72808=VECTOR ( 'NONE', #33660, 1000.000000000000000 ) ;
#72809=ORIENTED_EDGE ( 'NONE', *, *, #62846, .T. ) ;
#72811=CARTESIAN_POINT ( 'NONE',  ( -29.99451991528749417, 28.92564299267958816, 4.000000000000000000 ) ) ;
#72812=ORIENTED_EDGE ( 'NONE', *, *, #4991, .F. ) ;
#72813=VERTEX_POINT ( 'NONE', #68664 ) ;
#72814=VECTOR ( 'NONE', #8489, 1000.000000000000000 ) ;
#72815=LINE ( 'NONE', #61228, #59362 ) ;
#72816=CARTESIAN_POINT ( 'NONE',  ( -51.18398860626899705, 28.73617430169823095, 5.000000000000000000 ) ) ;
#72817=LINE ( 'NONE', #116970, #219 ) ;
#72818=EDGE_CURVE ( 'NONE', #83008, #116750, #4032, .T. ) ;
#72819=PLANE ( 'NONE',  #2358 ) ;
#72820=DIRECTION ( 'NONE',  ( 0.7071067811865486830, -0.7071067811865464625, -0.000000000000000000 ) ) ;
#72822=ADVANCED_FACE ( 'NONE', ( #14254 ), #25113, .F. ) ;
#72823=EDGE_CURVE ( 'NONE', #52532, #125922, #82390, .T. ) ;
#72825=DIRECTION ( 'NONE',  ( 0.7071067811865486830, -0.7071067811865464625, -0.000000000000000000 ) ) ;
#72827=DIRECTION ( 'NONE',  ( -0.7071067811865486830, -0.7071067811865464625, -0.000000000000000000 ) ) ;
#72828=PLANE ( 'NONE',  #14941 ) ;
#72830=ADVANCED_FACE ( 'NONE', ( #13514 ), #70810, .T. ) ;
#72832=EDGE_CURVE ( 'NONE', #109399, #18121, #114955, .T. ) ;
#72833=PLANE ( 'NONE',  #85338 ) ;
#72834=ORIENTED_EDGE ( 'NONE', *, *, #25432, .T. ) ;
#72835=ORIENTED_EDGE ( 'NONE', *, *, #22362, .F. ) ;
#72837=LINE ( 'NONE', #6754, #95613 ) ;
#72838=EDGE_CURVE ( 'NONE', #48106, #89121, #91807, .T. ) ;
#72839=DIRECTION ( 'NONE',  ( 0.6830127018922180770, -0.6830127018922204085, -0.2588190451025213501 ) ) ;
#72840=ORIENTED_EDGE ( 'NONE', *, *, #134515, .T. ) ;
#72843=EDGE_CURVE ( 'NONE', #110945, #97392, #60671, .T. ) ;
#72844=LINE ( 'NONE', #116997, #104547 ) ;
#72846=VERTEX_POINT ( 'NONE', #36715 ) ;
#72847=LINE ( 'NONE', #8210, #29358 ) ;
#72848=VERTEX_POINT ( 'NONE', #80958 ) ;
#72849=ORIENTED_EDGE ( 'NONE', *, *, #48352, .T. ) ;
#72850=FACE_OUTER_BOUND ( 'NONE', #129501, .T. ) ;
#72852=FACE_OUTER_BOUND ( 'NONE', #27633, .T. ) ;
#72853=PLANE ( 'NONE',  #97214 ) ;
#72854=CARTESIAN_POINT ( 'NONE',  ( 5.700255128608413102, -27.71228299555201957, 4.000000000000000000 ) ) ;
#72855=CARTESIAN_POINT ( 'NONE',  ( 7.828169399223479985, 0.7592924766157104211, 4.000000000000000000 ) ) ;
#72856=ORIENTED_EDGE ( 'NONE', *, *, #30269, .F. ) ;
#72857=CARTESIAN_POINT ( 'NONE',  ( 27.04658813629527714, 14.25929247661557042, 18.84478104361321726 ) ) ;
#72858=PLANE ( 'NONE',  #84832 ) ;
#72859=DIRECTION ( 'NONE',  ( -0.7071067811865487940, 0.7071067811865463515, -0.000000000000000000 ) ) ;
#72860=VECTOR ( 'NONE', #69880, 1000.000000000000000 ) ;
#72861=EDGE_CURVE ( 'NONE', #57345, #2265, #90387, .T. ) ;
#72862=DIRECTION ( 'NONE',  ( 0.7071067811865487940, 0.7071067811865463515, 0.000000000000000000 ) ) ;
#72863=VERTEX_POINT ( 'NONE', #59236 ) ;
#72864=VECTOR ( 'NONE', #140022, 1000.000000000000000 ) ;
#72865=ORIENTED_EDGE ( 'NONE', *, *, #72034, .T. ) ;
#72867=VECTOR ( 'NONE', #130009, 999.9999999999998863 ) ;
#72868=DIRECTION ( 'NONE',  ( 0.6830127018922181881, 0.6830127018922202975, -0.2588190451025214056 ) ) ;
#72869=DIRECTION ( 'NONE',  ( -1.000000000000000000, 0.000000000000000000, -0.000000000000000000 ) ) ;
#72870=ADVANCED_FACE ( 'NONE', ( #134635 ), #35330, .F. ) ;
#72871=DIRECTION ( 'NONE',  ( 0.6830127018922181881, 0.6830127018922202975, -0.2588190451025214056 ) ) ;
#72873=EDGE_LOOP ( 'NONE', ( #7134, #18975, #34579, #68269 ) ) ;
#72874=ORIENTED_EDGE ( 'NONE', *, *, #9550, .F. ) ;
#72875=DIRECTION ( 'NONE',  ( -0.7071067811865486830, 0.7071067811865464625, 0.000000000000000000 ) ) ;
#72876=ORIENTED_EDGE ( 'NONE', *, *, #12186, .F. ) ;
#72877=EDGE_CURVE ( 'NONE', #56699, #92397, #62785, .T. ) ;
#72878=EDGE_LOOP ( 'NONE', ( #134741, #76356, #126147, #92703 ) ) ;
#72879=VECTOR ( 'NONE', #112841, 1000.000000000000000 ) ;
#72880=CARTESIAN_POINT ( 'NONE',  ( 3.524001385854470314, 22.03583458319437582, 4.979811245910088502 ) ) ;
#72881=VERTEX_POINT ( 'NONE', #52591 ) ;
#72882=EDGE_CURVE ( 'NONE', #64418, #119637, #127295, .T. ) ;
#72884=CARTESIAN_POINT ( 'NONE',  ( -0.4892135623730947680, -27.52281430457055578, 5.000000000000000000 ) ) ;
#72886=FACE_BOUND ( 'NONE', #59929, .T. ) ;
#72888=CARTESIAN_POINT ( 'NONE',  ( -18.48921356237309510, -27.52281430457068367, 5.000000000000000000 ) ) ;
#72890=ORIENTED_EDGE ( 'NONE', *, *, #114260, .T. ) ;
#72891=VECTOR ( 'NONE', #41125, 1000.000000000000000 ) ;
#72893=VERTEX_POINT ( 'NONE', #63515 ) ;
#72895=AXIS2_PLACEMENT_3D ( 'NONE', #44223, #132678, #33369 ) ;
#72896=ORIENTED_EDGE ( 'NONE', *, *, #27883, .F. ) ;
#72900=EDGE_CURVE ( 'NONE', #49384, #10452, #75099, .T. ) ;
#72903=CARTESIAN_POINT ( 'NONE',  ( -57.18398860626899705, 28.73617430169827358, 5.000000000000000000 ) ) ;
#72904=VECTOR ( 'NONE', #27196, 1000.000000000000000 ) ;
#72905=CARTESIAN_POINT ( 'NONE',  ( 19.17183060077633883, 21.75929247661549937, 4.000000000000000000 ) ) ;
#72907=DIRECTION ( 'NONE',  ( 0.7071067811865486830, -0.7071067811865464625, -0.000000000000000000 ) ) ;
#72908=EDGE_CURVE ( 'NONE', #138159, #34174, #141022, .T. ) ;
#72909=DIRECTION ( 'NONE',  ( -0.3543493200069162685, -0.000000000000000000, -0.9351131265310288487 ) ) ;
#72910=DIRECTION ( 'NONE',  ( -0.6830127018922180770, -0.6830127018922204085, -0.2588190451025213501 ) ) ;
#72911=CARTESIAN_POINT ( 'NONE',  ( 31.49999999999977973, 1.466399257802244893, 5.000000000000000000 ) ) ;
#72912=PLANE ( 'NONE',  #109356 ) ;
#72913=ORIENTED_EDGE ( 'NONE', *, *, #121267, .F. ) ;
#72914=DIRECTION ( 'NONE',  ( 0.3543493200069162685, -0.000000000000000000, -0.9351131265310288487 ) ) ;
#72915=LINE ( 'NONE', #9728, #141511 ) ;
#72916=ORIENTED_EDGE ( 'NONE', *, *, #10173, .T. ) ;
#72917=EDGE_CURVE ( 'NONE', #72171, #13889, #129434, .T. ) ;
#72918=VERTEX_POINT ( 'NONE', #84538 ) ;
#72921=ORIENTED_EDGE ( 'NONE', *, *, #25216, .F. ) ;
#72924=ORIENTED_EDGE ( 'NONE', *, *, #117657, .T. ) ;
#72925=ORIENTED_EDGE ( 'NONE', *, *, #60544, .F. ) ;
#72926=CARTESIAN_POINT ( 'NONE',  ( 14.20710678118645021, -20.24070752338407786, 5.000000000000000000 ) ) ;
#72927=CARTESIAN_POINT ( 'NONE',  ( -4.828169399223501301, 3.759292476615676559, 4.000000000000000000 ) ) ;
#72929=ORIENTED_EDGE ( 'NONE', *, *, #142409, .T. ) ;
#72930=EDGE_LOOP ( 'NONE', ( #123411, #69797, #75450, #30884, #90105, #73072 ) ) ;
#72931=AXIS2_PLACEMENT_3D ( 'NONE', #46341, #91934, #57211 ) ;
#72933=FACE_OUTER_BOUND ( 'NONE', #133599, .T. ) ;
#72934=CARTESIAN_POINT ( 'NONE',  ( 74.99451991528749772, 28.92564299267990435, 4.000000000000000000 ) ) ;
#72935=ORIENTED_EDGE ( 'NONE', *, *, #25978, .F. ) ;
#72936=EDGE_CURVE ( 'NONE', #43329, #2860, #18508, .T. ) ;
#72937=PLANE ( 'NONE',  #20327 ) ;
#72938=ORIENTED_EDGE ( 'NONE', *, *, #80818, .F. ) ;
#72940=ORIENTED_EDGE ( 'NONE', *, *, #43658, .T. ) ;
#72941=ORIENTED_EDGE ( 'NONE', *, *, #10382, .T. ) ;
#72942=DIRECTION ( 'NONE',  ( -0.7071067811865486830, 0.7071067811865464625, 0.000000000000000000 ) ) ;
#72943=LINE ( 'NONE', #130150, #65522 ) ;
#72944=LINE ( 'NONE', #118534, #93424 ) ;
#72945=DIRECTION ( 'NONE',  ( -0.000000000000000000, -0.3543493200069152693, 0.9351131265310292928 ) ) ;
#72946=EDGE_CURVE ( 'NONE', #129515, #121901, #73644, .T. ) ;
#72947=ORIENTED_EDGE ( 'NONE', *, *, #54584, .T. ) ;
#72948=LINE ( 'NONE', #60645, #9394 ) ;
#72949=ORIENTED_EDGE ( 'NONE', *, *, #19759, .T. ) ;
#72950=CARTESIAN_POINT ( 'NONE',  ( -23.99999999999983302, 16.55218569542900298, 5.000000000000000000 ) ) ;
#72951=AXIS2_PLACEMENT_3D ( 'NONE', #139129, #39834, #40529 ) ;
#72953=DIRECTION ( 'NONE',  ( 1.000000000000000000, 0.000000000000000000, 0.000000000000000000 ) ) ;
#72954=CARTESIAN_POINT ( 'NONE',  ( 18.00548008471250583, 28.92564299267925776, 4.000000000000000000 ) ) ;
#72955=PLANE ( 'NONE',  #11923 ) ;
#72956=ORIENTED_EDGE ( 'NONE', *, *, #131907, .F. ) ;
#72957=VECTOR ( 'NONE', #139323, 1000.000000000000000 ) ;
#72958=ORIENTED_EDGE ( 'NONE', *, *, #28515, .F. ) ;
#72959=ORIENTED_EDGE ( 'NONE', *, *, #94726, .T. ) ;
#72960=DIRECTION ( 'NONE',  ( 1.000000000000000000, 0.000000000000000000, 0.000000000000000000 ) ) ;
#72961=CARTESIAN_POINT ( 'NONE',  ( 0.000000000000000000, 0.000000000000000000, 5.000000000000000000 ) ) ;
#72962=CARTESIAN_POINT ( 'NONE',  ( 22.73493329717935652, 12.75929247661558996, 18.34774599283950991 ) ) ;
#72963=FACE_OUTER_BOUND ( 'NONE', #99989, .T. ) ;
#72964=CARTESIAN_POINT ( 'NONE',  ( -23.24139925780185223, 21.72500000000000853, 5.000000000000000000 ) ) ;
#72966=DIRECTION ( 'NONE',  ( -0.7071067811865486830, -0.7071067811865464625, -0.000000000000000000 ) ) ;
#72967=FACE_OUTER_BOUND ( 'NONE', #54745, .T. ) ;
#72969=LINE ( 'NONE', #104830, #57152 ) ;
#72971=DIRECTION ( 'NONE',  ( 0.3543493200069162685, -0.000000000000000000, -0.9351131265310288487 ) ) ;
#72972=ORIENTED_EDGE ( 'NONE', *, *, #53003, .F. ) ;
#72974=VERTEX_POINT ( 'NONE', #118558 ) ;
#72975=DIRECTION ( 'NONE',  ( -0.7071067811865486830, -0.7071067811865464625, 0.000000000000000000 ) ) ;
#72976=CARTESIAN_POINT ( 'NONE',  ( 26.20710678118636494, 0.7592924766157120864, 5.000000000000000000 ) ) ;
#72978=FACE_OUTER_BOUND ( 'NONE', #44358, .T. ) ;
#72979=PLANE ( 'NONE',  #56559 ) ;
#72981=EDGE_LOOP ( 'NONE', ( #11501, #128860, #66474, #101073 ) ) ;
#72983=CARTESIAN_POINT ( 'NONE',  ( 2.510786437626908008, -27.52281430457053446, 5.000000000000000000 ) ) ;
#72984=CARTESIAN_POINT ( 'NONE',  ( 33.32816939922329880, -0.7407075233842753681, 4.000000000000000000 ) ) ;
#72985=DIRECTION ( 'NONE',  ( -0.6830127018922181881, 0.6830127018922202975, -0.2588190451025214056 ) ) ;
#72986=EDGE_CURVE ( 'NONE', #22682, #135194, #38872, .T. ) ;
#72988=EDGE_CURVE ( 'NONE', #30838, #97296, #41726, .T. ) ;
#72989=PLANE ( 'NONE',  #136549 ) ;
#72991=VECTOR ( 'NONE', #128528, 1000.000000000000227 ) ;
#72992=PLANE ( 'NONE',  #119992 ) ;
#72993=ORIENTED_EDGE ( 'NONE', *, *, #89719, .T. ) ;
#72994=EDGE_CURVE ( 'NONE', #25800, #103344, #49778, .T. ) ;
#72995=AXIS2_PLACEMENT_3D ( 'NONE', #35610, #66775, #79837 ) ;
#72996=CARTESIAN_POINT ( 'NONE',  ( 31.49999999999979039, 22.08746187583901843, 4.000000000000000000 ) ) ;
#72997=EDGE_CURVE ( 'NONE', #48791, #131882, #83093, .T. ) ;
#72998=CARTESIAN_POINT ( 'NONE',  ( -9.489213562373095101, -27.52281430457062328, 5.000000000000000000 ) ) ;
#73000=FACE_OUTER_BOUND ( 'NONE', #15738, .T. ) ;
#73001=EDGE_CURVE ( 'NONE', #47092, #89873, #105532, .T. ) ;
#73002=VERTEX_POINT ( 'NONE', #96767 ) ;
#73003=CARTESIAN_POINT ( 'NONE',  ( -11.99999999999991296, -16.06887692260766087, 4.000000000000000000 ) ) ;
#73005=VERTEX_POINT ( 'NONE', #6904 ) ;
#73008=LINE ( 'NONE', #62106, #65484 ) ;
#73009=CARTESIAN_POINT ( 'NONE',  ( 21.70710678118639692, -9.740707523384179112, 5.000000000000000000 ) ) ;
#73011=CARTESIAN_POINT ( 'NONE',  ( -3.134995737516202308, 3.759292476615678336, 15.36553568819726934 ) ) ;
#73013=LINE ( 'NONE', #117164, #65075 ) ;
#73014=DIRECTION ( 'NONE',  ( 1.000000000000000000, 0.000000000000000000, 0.000000000000000000 ) ) ;
#73015=DIRECTION ( 'NONE',  ( -0.7071067811865486830, 0.7071067811865464625, 0.000000000000000000 ) ) ;
#73018=LINE ( 'NONE', #62116, #124059 ) ;
#73019=CARTESIAN_POINT ( 'NONE',  ( -19.49999999999986144, -5.568876922607759461, 4.000000000000000000 ) ) ;
#73020=EDGE_CURVE ( 'NONE', #94372, #95699, #77246, .T. ) ;
#73021=DIRECTION ( 'NONE',  ( -0.3543493200069162685, -0.000000000000000000, -0.9351131265310288487 ) ) ;
#73022=ORIENTED_EDGE ( 'NONE', *, *, #27255, .F. ) ;
#73023=EDGE_LOOP ( 'NONE', ( #87601, #6487, #57326, #104300 ) ) ;
#73026=CARTESIAN_POINT ( 'NONE',  ( 57.48921356237308800, -27.52281430457095368, 5.000000000000000000 ) ) ;
#73027=CARTESIAN_POINT ( 'NONE',  ( 13.77149322861326652, 20.25929247661551358, 7.808871592221799496 ) ) ;
#73028=CARTESIAN_POINT ( 'NONE',  ( -17.29289321881334018, 20.25929247661551003, 5.000000000000000000 ) ) ;
#73029=EDGE_LOOP ( 'NONE', ( #6662, #8803, #118640, #92842 ) ) ;
#73031=LINE ( 'NONE', #117182, #118424 ) ;
#73032=VERTEX_POINT ( 'NONE', #131595 ) ;
#73033=CARTESIAN_POINT ( 'NONE',  ( 0.000000000000000000, 0.000000000000000000, 5.000000000000000000 ) ) ;
#73034=EDGE_CURVE ( 'NONE', #82669, #58856, #78641, .T. ) ;
#73035=DIRECTION ( 'NONE',  ( -0.6830127018922180770, -0.6830127018922204085, -0.2588190451025213501 ) ) ;
#73037=EDGE_CURVE ( 'NONE', #32044, #68720, #99656, .T. ) ;
#73038=EDGE_LOOP ( 'NONE', ( #137660, #136815, #10720, #61690 ) ) ;
#73039=EDGE_LOOP ( 'NONE', ( #57351, #26542, #88734, #28956, #102952 ) ) ;
#73040=CARTESIAN_POINT ( 'NONE',  ( 38.34328999833763874, 3.759292476615685441, 13.27625715073274115 ) ) ;
#73041=CARTESIAN_POINT ( 'NONE',  ( -39.48921356237310221, -27.52281430457082934, 5.000000000000000000 ) ) ;
#73042=CARTESIAN_POINT ( 'NONE',  ( 5.816011393731002066, 28.73617430169783304, 5.000000000000000000 ) ) ;
#73043=EDGE_CURVE ( 'NONE', #37329, #38295, #33029, .T. ) ;
#73044=CARTESIAN_POINT ( 'NONE',  ( -21.48921356237309155, -27.52281430457070499, 5.000000000000000000 ) ) ;
#73046=VECTOR ( 'NONE', #136615, 1000.000000000000000 ) ;
#73047=ORIENTED_EDGE ( 'NONE', *, *, #108895, .F. ) ;
#73048=ORIENTED_EDGE ( 'NONE', *, *, #79910, .F. ) ;
#73049=( BOUNDED_CURVE ( )  B_SPLINE_CURVE ( 3, ( #479, #44773, #75235, #54211 ),
 .UNSPECIFIED., .F., .T. ) 
 B_SPLINE_CURVE_WITH_KNOTS ( ( 4, 4 ),
 ( 2.779374508378133601, 4.199602562396808736 ),
 .UNSPECIFIED. ) 
 CURVE ( )  GEOMETRIC_REPRESENTATION_ITEM ( )  RATIONAL_B_SPLINE_CURVE ( ( 1.000000000000000000, 0.8388583629366690442, 0.8388583629366690442, 1.000000000000000000 ) ) 
 REPRESENTATION_ITEM ( '' )  );
#73051=AXIS2_PLACEMENT_3D ( 'NONE', #70707, #14851, #117022 ) ;
#73052=EDGE_CURVE ( 'NONE', #37692, #89916, #42472, .T. ) ;
#73053=ORIENTED_EDGE ( 'NONE', *, *, #25702, .T. ) ;
#73055=ORIENTED_EDGE ( 'NONE', *, *, #29446, .T. ) ;
#73056=VECTOR ( 'NONE', #139095, 1000.000000000000000 ) ;
#73058=PLANE ( 'NONE',  #105070 ) ;
#73059=CARTESIAN_POINT ( 'NONE',  ( 34.92499999999998295, 22.22500000000000142, 4.500000000000000888 ) ) ;
#73060=CARTESIAN_POINT ( 'NONE',  ( -29.01844734635652401, 18.75929247661553134, 20.33588619593449920 ) ) ;
#73061=CARTESIAN_POINT ( 'NONE',  ( -1.499999999999989120, 1.466399257802246670, 5.000000000000000000 ) ) ;
#73062=VERTEX_POINT ( 'NONE', #122853 ) ;
#73063=DIRECTION ( 'NONE',  ( 0.3543493200069163240, -0.000000000000000000, 0.9351131265310288487 ) ) ;
#73064=DIRECTION ( 'NONE',  ( 0.3543493200069162685, -0.000000000000000000, -0.9351131265310288487 ) ) ;
#73065=ORIENTED_EDGE ( 'NONE', *, *, #107927, .T. ) ;
#73066=LINE ( 'NONE', #139015, #96791 ) ;
#73067=EDGE_CURVE ( 'NONE', #141841, #65131, #121415, .T. ) ;
#73068=ORIENTED_EDGE ( 'NONE', *, *, #115112, .F. ) ;
#73069=EDGE_CURVE ( 'NONE', #20671, #135734, #75794, .T. ) ;
#73071=VERTEX_POINT ( 'NONE', #120688 ) ;
#73072=ORIENTED_EDGE ( 'NONE', *, *, #82799, .F. ) ;
#73074=VERTEX_POINT ( 'NONE', #9036 ) ;
#73077=CARTESIAN_POINT ( 'NONE',  ( -32.29298673570672662, -21.74070752338405299, 4.999753212805210012 ) ) ;
#73079=LINE ( 'NONE', #139761, #112017 ) ;
#73080=VECTOR ( 'NONE', #84647, 1000.000000000000114 ) ;
#73081=PLANE ( 'NONE',  #136648 ) ;
#73082=DIRECTION ( 'NONE',  ( -0.6830127018922180770, -0.6830127018922204085, -0.2588190451025213501 ) ) ;
#73087=EDGE_CURVE ( 'NONE', #8692, #130004, #110520, .T. ) ;
#73088=FACE_OUTER_BOUND ( 'NONE', #60747, .T. ) ;
#73089=LINE ( 'NONE', #93381, #22019 ) ;
#73090=VERTEX_POINT ( 'NONE', #11191 ) ;
#73091=ORIENTED_EDGE ( 'NONE', *, *, #120707, .F. ) ;
#73092=CARTESIAN_POINT ( 'NONE',  ( 78.18398860626899705, 28.73617430169841924, 5.000000000000000000 ) ) ;
#73094=CARTESIAN_POINT ( 'NONE',  ( -63.48921356237309510, -27.52281430457099631, 5.000000000000000000 ) ) ;
#73095=DIRECTION ( 'NONE',  ( -0.7071067811865486830, -0.7071067811865464625, 0.000000000000000000 ) ) ;
#73096=DIRECTION ( 'NONE',  ( 0.7071067811865486830, -0.7071067811865464625, -0.000000000000000000 ) ) ;
#73097=EDGE_CURVE ( 'NONE', #141006, #83058, #133741, .T. ) ;
#73098=DIRECTION ( 'NONE',  ( 1.000000000000000000, 0.000000000000000000, 0.000000000000000000 ) ) ;
#73099=ORIENTED_EDGE ( 'NONE', *, *, #57228, .T. ) ;
#73101=ORIENTED_EDGE ( 'NONE', *, *, #123377, .F. ) ;
#73103=CARTESIAN_POINT ( 'NONE',  ( -11.48334561358947070, 22.22500000000000142, 4.500000000000000888 ) ) ;
#73104=FACE_OUTER_BOUND ( 'NONE', #41906, .T. ) ;
#73106=VERTEX_POINT ( 'NONE', #1044 ) ;
#73107=ORIENTED_EDGE ( 'NONE', *, *, #61428, .F. ) ;
#73108=ORIENTED_EDGE ( 'NONE', *, *, #116243, .T. ) ;
#73109=LINE ( 'NONE', #115831, #61227 ) ;
#73110=PLANE ( 'NONE',  #39510 ) ;
#73111=CARTESIAN_POINT ( 'NONE',  ( 0.000000000000000000, 0.000000000000000000, 5.000000000000000000 ) ) ;
#73112=LINE ( 'NONE', #51348, #10205 ) ;
#73113=CARTESIAN_POINT ( 'NONE',  ( -33.70710678118629744, -6.740707523384209310, 5.000000000000000000 ) ) ;
#73114=FACE_OUTER_BOUND ( 'NONE', #26007, .T. ) ;
#73115=LINE ( 'NONE', #110506, #97409 ) ;
#73117=CARTESIAN_POINT ( 'NONE',  ( 0.000000000000000000, 0.000000000000000000, 5.000000000000000000 ) ) ;
#73118=CARTESIAN_POINT ( 'NONE',  ( 0.7933393645784738712, 21.75929247661549937, 4.998822639870705409 ) ) ;
#73120=ORIENTED_EDGE ( 'NONE', *, *, #142151, .T. ) ;
#73122=ADVANCED_FACE ( 'NONE', ( #97514 ), #55471, .F. ) ;
#73123=CARTESIAN_POINT ( 'NONE',  ( 45.48921356237309510, -27.52281430457087197, 5.000000000000000000 ) ) ;
#73124=ORIENTED_EDGE ( 'NONE', *, *, #80089, .T. ) ;
#73125=DIRECTION ( 'NONE',  ( 0.3543493200069162685, -0.000000000000000000, -0.9351131265310288487 ) ) ;
#73126=CARTESIAN_POINT ( 'NONE',  ( -25.49999999999982947, -15.29013452822856500, 0.3645803511609750913 ) ) ;
#73127=ORIENTED_EDGE ( 'NONE', *, *, #95009, .F. ) ;
#73129=DIRECTION ( 'NONE',  ( -0.000000000000000000, -0.3543493200069152693, 0.9351131265310292928 ) ) ;
#73130=ORIENTED_EDGE ( 'NONE', *, *, #33517, .F. ) ;
#73131=FACE_OUTER_BOUND ( 'NONE', #5511, .T. ) ;
#73133=VECTOR ( 'NONE', #8566, 1000.000000000000000 ) ;
#73135=EDGE_CURVE ( 'NONE', #56274, #42790, #88819, .T. ) ;
#73136=DIRECTION ( 'NONE',  ( 0.7071067811865487940, -0.7071067811865463515, 0.000000000000000000 ) ) ;
#73137=DIRECTION ( 'NONE',  ( 0.6830127018922180770, -0.6830127018922204085, -0.2588190451025213501 ) ) ;
#73139=EDGE_CURVE ( 'NONE', #26770, #109240, #33732, .T. ) ;
#73140=VECTOR ( 'NONE', #18774, 999.9999999999998863 ) ;
#73141=PLANE ( 'NONE',  #106999 ) ;
#73142=DIRECTION ( 'NONE',  ( -0.7071067811865486830, -0.7071067811865464625, 0.000000000000000000 ) ) ;
#73143=EDGE_CURVE ( 'NONE', #131775, #62699, #98941, .T. ) ;
#73147=DIRECTION ( 'NONE',  ( -0.000000000000000000, -0.3543493200069152693, 0.9351131265310292928 ) ) ;
#73148=CARTESIAN_POINT ( 'NONE',  ( -22.17183060077631396, -2.240707523384257716, 4.000000000000000000 ) ) ;
#73150=EDGE_CURVE ( 'NONE', #13156, #19842, #94316, .T. ) ;
#73151=ORIENTED_EDGE ( 'NONE', *, *, #26899, .T. ) ;
#73152=ORIENTED_EDGE ( 'NONE', *, *, #65780, .F. ) ;
#73154=ORIENTED_EDGE ( 'NONE', *, *, #5812, .T. ) ;
#73155=EDGE_CURVE ( 'NONE', #88478, #112059, #93620, .T. ) ;
#73157=CARTESIAN_POINT ( 'NONE',  ( 8.999999999999944933, 17.96639925780208102, 5.000000000000000000 ) ) ;
#73158=DIRECTION ( 'NONE',  ( -0.7071067811865487940, 0.7071067811865463515, 0.000000000000000000 ) ) ;
#73159=VERTEX_POINT ( 'NONE', #90216 ) ;
#73160=FACE_OUTER_BOUND ( 'NONE', #43268, .T. ) ;
#73161=CARTESIAN_POINT ( 'NONE',  ( 24.70710678118637205, -9.740707523384187994, 5.000000000000000000 ) ) ;
#73162=EDGE_CURVE ( 'NONE', #128274, #19220, #111995, .T. ) ;
#73163=CARTESIAN_POINT ( 'NONE',  ( 11.81601139373100651, 28.73617430169779041, 5.000000000000000000 ) ) ;
#73164=LINE ( 'NONE', #50671, #46660 ) ;
#73165=EDGE_CURVE ( 'NONE', #111466, #118332, #24944, .T. ) ;
#73166=DIRECTION ( 'NONE',  ( -0.000000000000000000, 0.000000000000000000, 1.000000000000000000 ) ) ;
#73167=DIRECTION ( 'NONE',  ( -0.7071067811865486830, -0.7071067811865464625, -0.000000000000000000 ) ) ;
#73168=DIRECTION ( 'NONE',  ( 0.7071067811865487940, 0.7071067811865463515, 0.000000000000000000 ) ) ;
#73169=CARTESIAN_POINT ( 'NONE',  ( 10.49999999999992717, -20.53675388469229546, 2.352720554255917751 ) ) ;
#73170=FACE_OUTER_BOUND ( 'NONE', #69426, .T. ) ;
#73172=DIRECTION ( 'NONE',  ( -1.000000000000000000, 0.000000000000000000, 0.000000000000000000 ) ) ;
#73173=EDGE_CURVE ( 'NONE', #33315, #23517, #82747, .T. ) ;
#73174=VECTOR ( 'NONE', #12858, 1000.000000000000000 ) ;
#73177=VERTEX_POINT ( 'NONE', #105194 ) ;
#73182=VECTOR ( 'NONE', #121795, 999.9999999999998863 ) ;
#73184=ORIENTED_EDGE ( 'NONE', *, *, #81814, .F. ) ;
#73186=DIRECTION ( 'NONE',  ( 1.000000000000000000, 0.000000000000000000, 0.000000000000000000 ) ) ;
#73188=ORIENTED_EDGE ( 'NONE', *, *, #112105, .T. ) ;
#73189=FACE_OUTER_BOUND ( 'NONE', #142407, .T. ) ;
#73190=VERTEX_POINT ( 'NONE', #127683 ) ;
#73191=CARTESIAN_POINT ( 'NONE',  ( -21.29974487139158512, -27.71228299555221142, 4.000000000000000000 ) ) ;
#73192=EDGE_CURVE ( 'NONE', #14419, #121472, #83459, .T. ) ;
#73193=LINE ( 'NONE', #52813, #137143 ) ;
#73194=LINE ( 'NONE', #9287, #99476 ) ;
#73195=EDGE_LOOP ( 'NONE', ( #53444, #4989, #10081, #53711 ) ) ;
#73196=ORIENTED_EDGE ( 'NONE', *, *, #96369, .F. ) ;
#73197=VERTEX_POINT ( 'NONE', #5133 ) ;
#73198=DIRECTION ( 'NONE',  ( -0.3543493200069162685, -0.000000000000000000, -0.9351131265310288487 ) ) ;
#73199=DIRECTION ( 'NONE',  ( -0.3543493200069164351, 0.000000000000000000, -0.9351131265310288487 ) ) ;
#73202=EDGE_CURVE ( 'NONE', #141613, #80963, #56916, .T. ) ;
#73203=VERTEX_POINT ( 'NONE', #72626 ) ;
#73204=VERTEX_POINT ( 'NONE', #101089 ) ;
#73205=DIRECTION ( 'NONE',  ( 0.7071067811865487940, 0.7071067811865463515, 0.000000000000000000 ) ) ;
#73207=ORIENTED_EDGE ( 'NONE', *, *, #90817, .F. ) ;
#73208=EDGE_LOOP ( 'NONE', ( #142608, #43343, #107696, #115470 ) ) ;
#73209=VECTOR ( 'NONE', #70530, 1000.000000000000000 ) ;
#73210=CARTESIAN_POINT ( 'NONE',  ( -11.99999999999991473, -0.4125381241607498639, 4.000000000000000000 ) ) ;
#73212=ORIENTED_EDGE ( 'NONE', *, *, #111933, .T. ) ;
#73213=CARTESIAN_POINT ( 'NONE',  ( 25.82816939922335209, 21.75929247661549581, 4.000000000000000000 ) ) ;
#73214=EDGE_CURVE ( 'NONE', #84066, #77643, #2468, .T. ) ;
#73215=CARTESIAN_POINT ( 'NONE',  ( 11.51078643762690490, -27.52281430457047406, 5.000000000000000000 ) ) ;
#73216=CYLINDRICAL_SURFACE ( 'NONE', #96983, 0.5000000000000004441 ) ;
#73218=ORIENTED_EDGE ( 'NONE', *, *, #58289, .F. ) ;
#73219=CARTESIAN_POINT ( 'NONE',  ( -4.499999999999976019, 22.08746187583903264, 4.000000000000000000 ) ) ;
#73220=FACE_BOUND ( 'NONE', #99599, .T. ) ;
#73222=LINE ( 'NONE', #62349, #96658 ) ;
#73225=CARTESIAN_POINT ( 'NONE',  ( 78.29974487139158157, -27.71228299555260577, 4.000000000000000000 ) ) ;
#73226=ORIENTED_EDGE ( 'NONE', *, *, #34838, .T. ) ;
#73227=DIRECTION ( 'NONE',  ( 0.7071067811865487940, 0.7071067811865463515, 0.000000000000000000 ) ) ;
#73228=ORIENTED_EDGE ( 'NONE', *, *, #33554, .F. ) ;
#73229=ORIENTED_EDGE ( 'NONE', *, *, #76056, .T. ) ;
#73230=EDGE_LOOP ( 'NONE', ( #17879, #117761, #52761, #122548, #124549 ) ) ;
#73233=DIRECTION ( 'NONE',  ( 0.6830127018922181881, 0.6830127018922202975, -0.2588190451025214056 ) ) ;
#73237=PLANE ( 'NONE',  #59844 ) ;
#73238=DIRECTION ( 'NONE',  ( -0.7071067811865486830, 0.7071067811865464625, 0.000000000000000000 ) ) ;
#73240=DIRECTION ( 'NONE',  ( 0.6830127018922181881, 0.6830127018922202975, -0.2588190451025214056 ) ) ;
#73241=CARTESIAN_POINT ( 'NONE',  ( -12.83829387547372924, -6.740707523384205757, 16.75550250614864112 ) ) ;
#73243=CARTESIAN_POINT ( 'NONE',  ( 10.49999999999993605, 4.087461875839200509, 4.000000000000000000 ) ) ;
#73244=LINE ( 'NONE', #74679, #98047 ) ;
#73246=ORIENTED_EDGE ( 'NONE', *, *, #39936, .T. ) ;
#73247=ORIENTED_EDGE ( 'NONE', *, *, #98030, .T. ) ;
#73248=VERTEX_POINT ( 'NONE', #24258 ) ;
#73249=EDGE_LOOP ( 'NONE', ( #85188, #31285, #118676, #53814 ) ) ;
#73251=EDGE_LOOP ( 'NONE', ( #9558, #133742, #94702, #113882 ) ) ;
#73252=ORIENTED_EDGE ( 'NONE', *, *, #67685, .F. ) ;
#73254=DIRECTION ( 'NONE',  ( 0.6830127018922181881, 0.6830127018922202975, -0.2588190451025214056 ) ) ;
#73255=ADVANCED_FACE ( 'NONE', ( #5854 ), #134457, .F. ) ;
#73256=VECTOR ( 'NONE', #138420, 1000.000000000000000 ) ;
#73257=EDGE_CURVE ( 'NONE', #48371, #140728, #112684, .T. ) ;
#73258=CARTESIAN_POINT ( 'NONE',  ( 1.499999999999990896, 19.39370406404967184, 1.459788787078198258 ) ) ;
#73259=ORIENTED_EDGE ( 'NONE', *, *, #142555, .T. ) ;
#73261=VERTEX_POINT ( 'NONE', #46779 ) ;
#73262=VECTOR ( 'NONE', #40896, 999.9999999999998863 ) ;
#73263=AXIS2_PLACEMENT_3D ( 'NONE', #85112, #30009, #74250 ) ;
#73264=CARTESIAN_POINT ( 'NONE',  ( -20.99999999999984368, 17.58746187583906462, 4.000000000000000000 ) ) ;
#73266=VECTOR ( 'NONE', #90664, 1000.000000000000000 ) ;
#73268=ORIENTED_EDGE ( 'NONE', *, *, #89538, .F. ) ;
#73271=DIRECTION ( 'NONE',  ( -0.000000000000000000, -0.3543493200069152693, 0.9351131265310292928 ) ) ;
#73272=DIRECTION ( 'NONE',  ( -0.7071067811865487940, 0.7071067811865463515, -0.000000000000000000 ) ) ;
#73273=EDGE_LOOP ( 'NONE', ( #133867, #61640, #124392, #215 ) ) ;
#73274=ORIENTED_EDGE ( 'NONE', *, *, #70924, .F. ) ;
#73276=ORIENTED_EDGE ( 'NONE', *, *, #18392, .T. ) ;
#73277=LINE ( 'NONE', #59553, #90287 ) ;
#73278=DIRECTION ( 'NONE',  ( -0.7071067811865486830, -0.7071067811865464625, -0.000000000000000000 ) ) ;
#73279=VECTOR ( 'NONE', #139841, 1000.000000000000000 ) ;
#73281=PLANE ( 'NONE',  #100469 ) ;
#73282=EDGE_CURVE ( 'NONE', #73190, #82074, #90961, .T. ) ;
#73283=ORIENTED_EDGE ( 'NONE', *, *, #128807, .T. ) ;
#73284=CARTESIAN_POINT ( 'NONE',  ( -10.49999999999992717, -1.533600742197722910, 5.000000000000000000 ) ) ;
#73285=CARTESIAN_POINT ( 'NONE',  ( 34.92499999999998295, -4.662012949885794733, -5.188494296035330855 ) ) ;
#73286=CARTESIAN_POINT ( 'NONE',  ( 6.328169399223488867, 11.25929247661560595, 4.000000000000000000 ) ) ;
#73288=CARTESIAN_POINT ( 'NONE',  ( -66.18398860626901126, 28.73617430169833753, 5.000000000000000000 ) ) ;
#73289=CARTESIAN_POINT ( 'NONE',  ( -5.999999999999956479, 18.08204922493373346, 0.9627537363045027830 ) ) ;
#73290=EDGE_LOOP ( 'NONE', ( #48468, #71451, #73546, #93070 ) ) ;
#73292=EDGE_LOOP ( 'NONE', ( #52663, #37207, #45699, #132720 ) ) ;
#73293=DIRECTION ( 'NONE',  ( 0.7071067811865487940, 0.7071067811865463515, 0.000000000000000000 ) ) ;
#73294=LINE ( 'NONE', #98587, #73872 ) ;
#73295=EDGE_LOOP ( 'NONE', ( #31799, #120302, #10272, #70897 ) ) ;
#73296=DIRECTION ( 'NONE',  ( 0.6830127018922181881, 0.6830127018922202975, -0.2588190451025214056 ) ) ;
#73297=CARTESIAN_POINT ( 'NONE',  ( 13.74845587132416291, -11.24070752338416490, 10.39518518046006079 ) ) ;
#73298=EDGE_CURVE ( 'NONE', #44162, #16196, #131340, .T. ) ;
#73300=CARTESIAN_POINT ( 'NONE',  ( 81.18398860626899705, 28.73617430169844056, 5.000000000000000000 ) ) ;
#73301=CARTESIAN_POINT ( 'NONE',  ( -54.18398860626899705, 28.73617430169825226, 5.000000000000000000 ) ) ;
#73303=CARTESIAN_POINT ( 'NONE',  ( 34.42499999999998295, -19.45860074219776692, 5.000000000000000000 ) ) ;
#73304=CARTESIAN_POINT ( 'NONE',  ( 1.499999999999997780, -14.94781430457067728, 5.000000000000000000 ) ) ;
#73306=DIRECTION ( 'NONE',  ( -0.7071067811865486830, -0.7071067811865464625, 0.000000000000000000 ) ) ;
#73307=PLANE ( 'NONE',  #53642 ) ;
#73309=DIRECTION ( 'NONE',  ( 0.6830127018922180770, -0.6830127018922204085, -0.2588190451025213501 ) ) ;
#73310=DIRECTION ( 'NONE',  ( -0.7071067811865487940, 0.7071067811865463515, 0.000000000000000000 ) ) ;
#73311=EDGE_CURVE ( 'NONE', #127430, #131000, #3469, .T. ) ;
#73312=EDGE_LOOP ( 'NONE', ( #33625, #25393, #59330, #42979 ) ) ;
#73313=EDGE_CURVE ( 'NONE', #9187, #93841, #25971, .T. ) ;
#73314=( BOUNDED_CURVE ( )  B_SPLINE_CURVE ( 3, ( #15534, #59815, #126463, #5388 ),
 .UNSPECIFIED., .F., .T. ) 
 B_SPLINE_CURVE_WITH_KNOTS ( ( 4, 4 ),
 ( 2.779374508378134045, 4.199602562396851368 ),
 .UNSPECIFIED. ) 
 CURVE ( )  GEOMETRIC_REPRESENTATION_ITEM ( )  RATIONAL_B_SPLINE_CURVE ( ( 1.000000000000000000, 0.8388583629366599403, 0.8388583629366599403, 1.000000000000000000 ) ) 
 REPRESENTATION_ITEM ( '' )  );
#73315=ORIENTED_EDGE ( 'NONE', *, *, #66068, .F. ) ;
#73318=ORIENTED_EDGE ( 'NONE', *, *, #69750, .F. ) ;
#73319=ORIENTED_EDGE ( 'NONE', *, *, #106985, .F. ) ;
#73320=ORIENTED_EDGE ( 'NONE', *, *, #34878, .F. ) ;
#73322=CARTESIAN_POINT ( 'NONE',  ( 4.499999999999976019, 19.46639925780205616, 5.000000000000000000 ) ) ;
#73323=CARTESIAN_POINT ( 'NONE',  ( 18.29974487139159223, -27.71228299555219010, 4.000000000000000000 ) ) ;
#73327=LINE ( 'NONE', #140015, #53292 ) ;
#73328=ADVANCED_FACE ( 'NONE', ( #45090 ), #125285, .F. ) ;
#73329=DIRECTION ( 'NONE',  ( 0.7071067811865486830, -0.7071067811865464625, -0.000000000000000000 ) ) ;
#73333=VERTEX_POINT ( 'NONE', #81081 ) ;
#73334=EDGE_CURVE ( 'NONE', #119622, #91654, #44356, .T. ) ;
#73336=CARTESIAN_POINT ( 'NONE',  ( -50.99451991528749062, 28.92564299267973738, 4.000000000000000000 ) ) ;
#73337=CARTESIAN_POINT ( 'NONE',  ( 34.49999999999975842, 10.94296225409029510, -9.576120664313178210 ) ) ;
#73338=PLANE ( 'NONE',  #16790 ) ;
#73339=PLANE ( 'NONE',  #121764 ) ;
#73341=ADVANCED_FACE ( 'NONE', ( #87123 ), #102827, .F. ) ;
#73342=AXIS2_PLACEMENT_3D ( 'NONE', #9530, #29871, #98009 ) ;
#73343=DIRECTION ( 'NONE',  ( -0.7071067811865486830, -0.7071067811865464625, -0.000000000000000000 ) ) ;
#73345=ORIENTED_EDGE ( 'NONE', *, *, #107749, .F. ) ;
#73346=ORIENTED_EDGE ( 'NONE', *, *, #136759, .T. ) ;
#73348=AXIS2_PLACEMENT_3D ( 'NONE', #92417, #48958, #72164 ) ;
#73349=ORIENTED_EDGE ( 'NONE', *, *, #73732, .T. ) ;
#73350=DIRECTION ( 'NONE',  ( -0.6830127018922180770, -0.6830127018922204085, -0.2588190451025213501 ) ) ;
#73351=LINE ( 'NONE', #129130, #96429 ) ;
#73352=EDGE_CURVE ( 'NONE', #108369, #60317, #70239, .T. ) ;
#73353=DIRECTION ( 'NONE',  ( -0.000000000000000000, -0.3543493200069152693, 0.9351131265310292928 ) ) ;
#73354=DIRECTION ( 'NONE',  ( 0.7071067811865486830, -0.7071067811865464625, -0.000000000000000000 ) ) ;
#73355=DIRECTION ( 'NONE',  ( -1.000000000000000000, 0.000000000000000000, 0.000000000000000000 ) ) ;
#73356=LINE ( 'NONE', #138605, #81216 ) ;
#73358=VECTOR ( 'NONE', #38258, 1000.000000000000000 ) ;
#73359=VERTEX_POINT ( 'NONE', #88569 ) ;
#73360=CARTESIAN_POINT ( 'NONE',  ( -34.92500000000001137, 18.20450307870169482, 3.476483422452869565 ) ) ;
#73361=ORIENTED_EDGE ( 'NONE', *, *, #14239, .T. ) ;
#73362=EDGE_CURVE ( 'NONE', #128274, #120044, #66102, .T. ) ;
#73364=DIRECTION ( 'NONE',  ( 0.7071067811865487940, 0.7071067811865463515, 0.000000000000000000 ) ) ;
#73365=DIRECTION ( 'NONE',  ( 1.000000000000000000, 0.000000000000000000, 0.000000000000000000 ) ) ;
#73366=EDGE_LOOP ( 'NONE', ( #57325, #3835, #79293, #49556 ) ) ;
#73367=AXIS2_PLACEMENT_3D ( 'NONE', #139541, #27876, #37342 ) ;
#73369=EDGE_LOOP ( 'NONE', ( #117107, #43470, #60310, #73944 ) ) ;
#73370=LINE ( 'NONE', #29827, #26237 ) ;
#73372=CARTESIAN_POINT ( 'NONE',  ( -54.48921356237310221, -27.52281430457093236, 5.000000000000000000 ) ) ;
#73373=EDGE_CURVE ( 'NONE', #45800, #78583, #10948, .T. ) ;
#73374=EDGE_CURVE ( 'NONE', #94538, #87694, #21141, .T. ) ;
#73375=CARTESIAN_POINT ( 'NONE',  ( 5.999999999999963585, -10.06887692260771061, 4.000000000000000000 ) ) ;
#73376=VECTOR ( 'NONE', #39681, 1000.000000000000000 ) ;
#73379=VECTOR ( 'NONE', #70163, 1000.000000000000227 ) ;
#73382=CARTESIAN_POINT ( 'NONE',  ( 33.29974487139158867, -27.71228299555229313, 4.000000000000000000 ) ) ;
#73383=VECTOR ( 'NONE', #34647, 1000.000000000000000 ) ;
#73384=CARTESIAN_POINT ( 'NONE',  ( 3.489213562373097322, -27.52281430457057709, 5.000000000000000000 ) ) ;
#73385=ORIENTED_EDGE ( 'NONE', *, *, #123024, .T. ) ;
#73386=ORIENTED_EDGE ( 'NONE', *, *, #90756, .T. ) ;
#73387=AXIS2_PLACEMENT_3D ( 'NONE', #105937, #63218, #137899 ) ;
#73388=ORIENTED_EDGE ( 'NONE', *, *, #5294, .T. ) ;
#73390=EDGE_LOOP ( 'NONE', ( #132288, #78655, #87510, #61570 ) ) ;
#73391=CARTESIAN_POINT ( 'NONE',  ( 3.489213562373097322, -27.52281430457057709, 5.000000000000000000 ) ) ;
#73392=FACE_BOUND ( 'NONE', #127083, .T. ) ;
#73393=CARTESIAN_POINT ( 'NONE',  ( 18.29974487139159223, -27.71228299555219010, 4.000000000000000000 ) ) ;
#73394=DIRECTION ( 'NONE',  ( 0.6830127018922180770, -0.6830127018922204085, -0.2588190451025213501 ) ) ;
#73397=ORIENTED_EDGE ( 'NONE', *, *, #10993, .F. ) ;
#73398=VECTOR ( 'NONE', #132822, 1000.000000000000000 ) ;
#73399=ORIENTED_EDGE ( 'NONE', *, *, #57929, .T. ) ;
#73400=CARTESIAN_POINT ( 'NONE',  ( -32.29289321881322650, -15.74070752338412760, 5.000000000000000000 ) ) ;
#73401=ORIENTED_EDGE ( 'NONE', *, *, #3516, .T. ) ;
#73403=VECTOR ( 'NONE', #83977, 1000.000000000000227 ) ;
#73405=DIRECTION ( 'NONE',  ( -0.7071067811865487940, 0.7071067811865463515, 0.000000000000000000 ) ) ;
#73406=DIRECTION ( 'NONE',  ( 0.7071067811865487940, 0.7071067811865463515, 0.000000000000000000 ) ) ;
#73408=DIRECTION ( 'NONE',  ( 0.7071067811865487940, 0.7071067811865463515, 0.000000000000000000 ) ) ;
#73411=FACE_OUTER_BOUND ( 'NONE', #135750, .T. ) ;
#73414=DIRECTION ( 'NONE',  ( -0.7071067811865486830, -0.7071067811865464625, 0.000000000000000000 ) ) ;
#73415=ORIENTED_EDGE ( 'NONE', *, *, #38820, .T. ) ;
#73416=VECTOR ( 'NONE', #8177, 1000.000000000000000 ) ;
#73417=ORIENTED_EDGE ( 'NONE', *, *, #32105, .F. ) ;
#73418=DIRECTION ( 'NONE',  ( -0.000000000000000000, 0.000000000000000000, 1.000000000000000000 ) ) ;
#73419=FACE_OUTER_BOUND ( 'NONE', #13669, .T. ) ;
#73420=EDGE_LOOP ( 'NONE', ( #37883, #21267, #75239 ) ) ;
#73421=ORIENTED_EDGE ( 'NONE', *, *, #114155, .T. ) ;
#73422=ORIENTED_EDGE ( 'NONE', *, *, #132915, .T. ) ;
#73423=DIRECTION ( 'NONE',  ( 0.7071067811865486830, -0.7071067811865464625, -0.000000000000000000 ) ) ;
#73424=VECTOR ( 'NONE', #137214, 1000.000000000000000 ) ;
#73425=EDGE_CURVE ( 'NONE', #82074, #27289, #76994, .T. ) ;
#73426=EDGE_CURVE ( 'NONE', #92047, #92458, #54516, .T. ) ;
#73428=ORIENTED_EDGE ( 'NONE', *, *, #121125, .F. ) ;
#73429=CARTESIAN_POINT ( 'NONE',  ( -20.99999999999984368, -7.447814304570752775, 5.000000000000000000 ) ) ;
#73430=CARTESIAN_POINT ( 'NONE',  ( 14.99999999999990052, -6.412538124160687580, 4.000000000000000000 ) ) ;
#73432=DIRECTION ( 'NONE',  ( -0.000000000000000000, 0.3543493200069153248, 0.9351131265310292928 ) ) ;
#73436=EDGE_CURVE ( 'NONE', #43782, #130838, #135464, .T. ) ;
#73438=DIRECTION ( 'NONE',  ( -0.000000000000000000, -0.3543493200069152693, 0.9351131265310292928 ) ) ;
#73439=CARTESIAN_POINT ( 'NONE',  ( 2.292893218813439216, 20.25929247661551713, 5.000000000000000000 ) ) ;
#73440=ORIENTED_EDGE ( 'NONE', *, *, #64806, .F. ) ;
#73441=LINE ( 'NONE', #4525, #97953 ) ;
#73444=PLANE ( 'NONE',  #79472 ) ;
#73445=DIRECTION ( 'NONE',  ( -0.7071067811865486830, -0.7071067811865464625, -0.000000000000000000 ) ) ;
#73446=ADVANCED_FACE ( 'NONE', ( #21856 ), #132805, .F. ) ;
#73447=VERTEX_POINT ( 'NONE', #80377 ) ;
#73448=AXIS2_PLACEMENT_3D ( 'NONE', #29330, #83019, #39529 ) ;
#73449=LINE ( 'NONE', #115467, #79655 ) ;
#73450=LINE ( 'NONE', #18301, #16369 ) ;
#73451=CARTESIAN_POINT ( 'NONE',  ( -13.49999999999990052, 6.052185695429106893, 5.000000000000000000 ) ) ;
#73452=ORIENTED_EDGE ( 'NONE', *, *, #108765, .F. ) ;
#73453=ADVANCED_FACE ( 'NONE', ( #124566 ), #135664, .F. ) ;
#73454=DIRECTION ( 'NONE',  ( -0.000000000000000000, 0.000000000000000000, 1.000000000000000000 ) ) ;
#73455=DIRECTION ( 'NONE',  ( -0.7071067811865487940, 0.7071067811865463515, 0.000000000000000000 ) ) ;
#73456=DIRECTION ( 'NONE',  ( -0.6830127018922181881, 0.6830127018922202975, -0.2588190451025214056 ) ) ;
#73457=DIRECTION ( 'NONE',  ( -0.000000000000000000, -0.3543493200069152693, 0.9351131265310292928 ) ) ;
#73458=VECTOR ( 'NONE', #1299, 1000.000000000000000 ) ;
#73461=ORIENTED_EDGE ( 'NONE', *, *, #84309, .F. ) ;
#73462=LINE ( 'NONE', #116239, #3173 ) ;
#73463=VECTOR ( 'NONE', #66420, 1000.000000000000000 ) ;
#73464=AXIS2_PLACEMENT_3D ( 'NONE', #68422, #90124, #35071 ) ;
#73466=DIRECTION ( 'NONE',  ( 0.7071067811865486830, -0.7071067811865464625, -0.000000000000000000 ) ) ;
#73468=LINE ( 'NONE', #82225, #120072 ) ;
#73470=EDGE_LOOP ( 'NONE', ( #43563, #57004, #23805, #2059 ) ) ;
#73473=LINE ( 'NONE', #91808, #11885 ) ;
#73475=CARTESIAN_POINT ( 'NONE',  ( 0.000000000000000000, 0.000000000000000000, 5.000000000000000000 ) ) ;
#73478=ADVANCED_FACE ( 'NONE', ( #12434 ), #45120, .T. ) ;
#73479=EDGE_CURVE ( 'NONE', #71697, #25861, #89989, .T. ) ;
#73480=ORIENTED_EDGE ( 'NONE', *, *, #71013, .F. ) ;
#73481=DIRECTION ( 'NONE',  ( 0.7071067811865486830, -0.7071067811865464625, -0.000000000000000000 ) ) ;
#73482=EDGE_LOOP ( 'NONE', ( #57183, #117200, #105332, #72064 ) ) ;
#73483=EDGE_LOOP ( 'NONE', ( #31178, #113472, #11596, #15922 ) ) ;
#73484=CARTESIAN_POINT ( 'NONE',  ( -7.499999999999954703, 3.653845994658382779, -4.504631822206354386 ) ) ;
#73486=CARTESIAN_POINT ( 'NONE',  ( 21.60486233187507921, 21.75929247661549226, 21.32995629748181443 ) ) ;
#73487=PLANE ( 'NONE',  #23431 ) ;
#73488=DIRECTION ( 'NONE',  ( -0.6830127018922180770, -0.6830127018922204085, -0.2588190451025213501 ) ) ;
#73489=EDGE_CURVE ( 'NONE', #96482, #95547, #17413, .T. ) ;
#73492=EDGE_LOOP ( 'NONE', ( #106106, #122240, #76945, #55718, #83057 ) ) ;
#73494=FACE_OUTER_BOUND ( 'NONE', #136426, .T. ) ;
#73495=DIRECTION ( 'NONE',  ( 0.3543493200069162685, -0.000000000000000000, -0.9351131265310288487 ) ) ;
#73497=LINE ( 'NONE', #95942, #47307 ) ;
#73498=PLANE ( 'NONE',  #6779 ) ;
#73499=LINE ( 'NONE', #53140, #128391 ) ;
#73500=( BOUNDED_CURVE ( )  B_SPLINE_CURVE ( 3, ( #26506, #70751, #125096, #4686 ),
 .UNSPECIFIED., .F., .T. ) 
 B_SPLINE_CURVE_WITH_KNOTS ( ( 4, 4 ),
 ( 4.350170835173024386, 4.500739107949264017 ),
 .UNSPECIFIED. ) 
 CURVE ( )  GEOMETRIC_REPRESENTATION_ITEM ( )  RATIONAL_B_SPLINE_CURVE ( ( 1.000000000000000000, 0.9981116584018943083, 0.9981116584018943083, 1.000000000000000000 ) ) 
 REPRESENTATION_ITEM ( '' )  );
#73504=PLANE ( 'NONE',  #99394 ) ;
#73505=EDGE_LOOP ( 'NONE', ( #85808, #113104, #53282, #96153 ) ) ;
#73506=ORIENTED_EDGE ( 'NONE', *, *, #109095, .F. ) ;
#73508=EDGE_CURVE ( 'NONE', #46464, #49172, #14588, .T. ) ;
#73509=CARTESIAN_POINT ( 'NONE',  ( 34.92499999999998295, -12.18334561358941137, 4.500000000000000888 ) ) ;
#73510=DIRECTION ( 'NONE',  ( -0.000000000000000000, -0.3543493200069152693, 0.9351131265310292928 ) ) ;
#73511=VECTOR ( 'NONE', #24315, 999.9999999999998863 ) ;
#73512=CARTESIAN_POINT ( 'NONE',  ( 45.18398860626900415, 28.73617430169818832, 5.000000000000000000 ) ) ;
#73513=ORIENTED_EDGE ( 'NONE', *, *, #40173, .F. ) ;
#73514=EDGE_CURVE ( 'NONE', #84503, #29420, #45980, .T. ) ;
#73515=DIRECTION ( 'NONE',  ( -0.7071067811865486830, -0.7071067811865464625, -0.000000000000000000 ) ) ;
#73517=ORIENTED_EDGE ( 'NONE', *, *, #22513, .F. ) ;
#73518=VECTOR ( 'NONE', #53527, 1000.000000000000000 ) ;
#73521=EDGE_LOOP ( 'NONE', ( #20347, #135787, #82282, #126443 ) ) ;
#73522=DIRECTION ( 'NONE',  ( 0.3543493200069162685, -0.000000000000000000, -0.9351131265310288487 ) ) ;
#73524=LINE ( 'NONE', #62647, #127672 ) ;
#73525=VECTOR ( 'NONE', #62163, 1000.000000000000000 ) ;
#73526=FACE_OUTER_BOUND ( 'NONE', #66794, .T. ) ;
#73527=CARTESIAN_POINT ( 'NONE',  ( 9.183988606268997046, 28.73617430169793607, 5.000000000000000000 ) ) ;
#73528=LINE ( 'NONE', #127167, #92788 ) ;
#73529=PLANE ( 'NONE',  #63813 ) ;
#73530=VERTEX_POINT ( 'NONE', #78427 ) ;
#73531=CARTESIAN_POINT ( 'NONE',  ( -19.49999999999986855, 21.43112307739196609, 4.000000000000000000 ) ) ;
#73532=LINE ( 'NONE', #95261, #100307 ) ;
#73533=EDGE_CURVE ( 'NONE', #124853, #127004, #124774, .T. ) ;
#73534=LINE ( 'NONE', #27151, #106299 ) ;
#73535=EDGE_CURVE ( 'NONE', #22717, #133731, #24042, .T. ) ;
#73536=ORIENTED_EDGE ( 'NONE', *, *, #79475, .F. ) ;
#73537=EDGE_CURVE ( 'NONE', #10426, #67860, #56717, .T. ) ;
#73538=ORIENTED_EDGE ( 'NONE', *, *, #116848, .T. ) ;
#73539=VECTOR ( 'NONE', #90317, 999.9999999999998863 ) ;
#73542=DIRECTION ( 'NONE',  ( 0.6830127018922180770, -0.6830127018922204085, -0.2588190451025213501 ) ) ;
#73544=PLANE ( 'NONE',  #73367 ) ;
#73546=ORIENTED_EDGE ( 'NONE', *, *, #22332, .F. ) ;
#73547=PLANE ( 'NONE',  #130208 ) ;
#73548=EDGE_CURVE ( 'NONE', #88210, #49923, #34933, .T. ) ;
#73549=EDGE_LOOP ( 'NONE', ( #6152, #47391, #106576, #109590 ) ) ;
#73550=VERTEX_POINT ( 'NONE', #1532 ) ;
#73551=DIRECTION ( 'NONE',  ( -0.6830127018922181881, 0.6830127018922202975, -0.2588190451025214056 ) ) ;
#73552=ORIENTED_EDGE ( 'NONE', *, *, #101235, .T. ) ;
#73553=LINE ( 'NONE', #120579, #82670 ) ;
#73554=DIRECTION ( 'NONE',  ( 0.3543493200069162685, -0.000000000000000000, -0.9351131265310288487 ) ) ;
#73556=FACE_BOUND ( 'NONE', #29264, .T. ) ;
#73557=CARTESIAN_POINT ( 'NONE',  ( -17.99451991528748351, 28.92564299267950645, 4.000000000000000000 ) ) ;
#73558=CARTESIAN_POINT ( 'NONE',  ( -14.99999999999989697, 13.93112307739204070, 4.000000000000000000 ) ) ;
#73559=DIRECTION ( 'NONE',  ( -0.7071067811865486830, -0.7071067811865464625, -0.000000000000000000 ) ) ;
#73561=AXIS2_PLACEMENT_3D ( 'NONE', #25234, #1324, #58655 ) ;
#73562=VECTOR ( 'NONE', #140756, 1000.000000000000000 ) ;
#73563=FACE_OUTER_BOUND ( 'NONE', #37977, .T. ) ;
#73565=VERTEX_POINT ( 'NONE', #45815 ) ;
#73568=VERTEX_POINT ( 'NONE', #24744 ) ;
#73569=CARTESIAN_POINT ( 'NONE',  ( -23.01088028653932582, -22.02621442084247860, 4.990779571109221990 ) ) ;
#73570=PLANE ( 'NONE',  #134619 ) ;
#73571=EDGE_CURVE ( 'NONE', #87041, #94289, #124071, .T. ) ;
#73572=CARTESIAN_POINT ( 'NONE',  ( -33.29974487139158867, -27.71228299555229313, 4.000000000000000000 ) ) ;
#73573=CARTESIAN_POINT ( 'NONE',  ( 45.48921356237309510, -27.52281430457087197, 5.000000000000000000 ) ) ;
#73574=CARTESIAN_POINT ( 'NONE',  ( 7.208502053023265077, 22.22500000000000142, 20.96595896090590117 ) ) ;
#73575=CARTESIAN_POINT ( 'NONE',  ( 21.18398860626899349, 28.73617430169802134, 5.000000000000000000 ) ) ;
#73576=DIRECTION ( 'NONE',  ( -0.7071067811865486830, -0.7071067811865464625, -0.000000000000000000 ) ) ;
#73577=DIRECTION ( 'NONE',  ( 0.7071067811865487940, 0.7071067811865463515, 0.000000000000000000 ) ) ;
#73578=PLANE ( 'NONE',  #19548 ) ;
#73579=CARTESIAN_POINT ( 'NONE',  ( -22.82816939922336630, 12.75929247661558996, 4.000000000000000000 ) ) ;
#73580=FACE_OUTER_BOUND ( 'NONE', #98016, .T. ) ;
#73581=LINE ( 'NONE', #137413, #7506 ) ;
#73582=ORIENTED_EDGE ( 'NONE', *, *, #61450, .T. ) ;
#73583=CARTESIAN_POINT ( 'NONE',  ( -22.49999999999985079, -12.66682484999668290, -0.6294897503864461674 ) ) ;
#73584=CARTESIAN_POINT ( 'NONE',  ( 34.92499999999998295, -12.53194198458144903, -8.170704600677598961 ) ) ;
#73587=ORIENTED_EDGE ( 'NONE', *, *, #95744, .F. ) ;
#73588=EDGE_CURVE ( 'NONE', #69767, #124649, #126210, .T. ) ;
#73591=VECTOR ( 'NONE', #109582, 1000.000000000000000 ) ;
#73592=EDGE_LOOP ( 'NONE', ( #92900, #5753, #2615, #36212 ) ) ;
#73594=EDGE_CURVE ( 'NONE', #72640, #30768, #7242, .T. ) ;
#73597=ORIENTED_EDGE ( 'NONE', *, *, #28407, .F. ) ;
#73598=EDGE_CURVE ( 'NONE', #8801, #62928, #139962, .T. ) ;
#73599=CARTESIAN_POINT ( 'NONE',  ( -27.29974487139158512, -27.71228299555225405, 4.000000000000000000 ) ) ;
#73600=EDGE_LOOP ( 'NONE', ( #43753, #116731, #73101, #85644, #16331 ) ) ;
#73601=DIRECTION ( 'NONE',  ( 0.3543493200069162685, -0.000000000000000000, -0.9351131265310288487 ) ) ;
#73602=CARTESIAN_POINT ( 'NONE',  ( 34.92499999999998295, -3.183345613589516621, 4.500000000000000888 ) ) ;
#73603=CARTESIAN_POINT ( 'NONE',  ( 7.171830600776422315, 9.759292476615620160, 4.000000000000000000 ) ) ;
#73604=ORIENTED_EDGE ( 'NONE', *, *, #39331, .T. ) ;
#73605=ORIENTED_EDGE ( 'NONE', *, *, #132415, .F. ) ;
#73606=DIRECTION ( 'NONE',  ( 0.7071067811865487940, 0.7071067811865463515, 0.000000000000000000 ) ) ;
#73607=EDGE_CURVE ( 'NONE', #45742, #56014, #5096, .T. ) ;
#73608=ORIENTED_EDGE ( 'NONE', *, *, #138226, .T. ) ;
#73609=LINE ( 'NONE', #30084, #4125 ) ;
#73610=VERTEX_POINT ( 'NONE', #16723 ) ;
#73611=ORIENTED_EDGE ( 'NONE', *, *, #9486, .T. ) ;
#73612=ORIENTED_EDGE ( 'NONE', *, *, #109350, .T. ) ;
#73613=ORIENTED_EDGE ( 'NONE', *, *, #86206, .F. ) ;
#73614=DIRECTION ( 'NONE',  ( 0.7071067811865487940, 0.7071067811865463515, -0.000000000000000000 ) ) ;
#73615=EDGE_CURVE ( 'NONE', #71971, #17986, #84164, .T. ) ;
#73616=LINE ( 'NONE', #18477, #40062 ) ;
#73619=DIRECTION ( 'NONE',  ( -0.6830127018922181881, 0.6830127018922202975, -0.2588190451025214056 ) ) ;
#73620=EDGE_LOOP ( 'NONE', ( #45060, #14664, #18937, #20606 ) ) ;
#73621=DIRECTION ( 'NONE',  ( -0.6830127018922181881, 0.6830127018922202975, -0.2588190451025214056 ) ) ;
#73623=EDGE_CURVE ( 'NONE', #48695, #115675, #26886, .T. ) ;
#73624=DIRECTION ( 'NONE',  ( -0.000000000000000000, 0.3543493200069153248, 0.9351131265310292928 ) ) ;
#73626=CARTESIAN_POINT ( 'NONE',  ( 8.475998614145455079, 22.03583458319438293, 4.979811245910090278 ) ) ;
#73627=ORIENTED_EDGE ( 'NONE', *, *, #78191, .T. ) ;
#73628=CARTESIAN_POINT ( 'NONE',  ( 23.47599861414535027, 22.03583458319437227, 4.979811245910089390 ) ) ;
#73629=VECTOR ( 'NONE', #96536, 1000.000000000000000 ) ;
#73630=CARTESIAN_POINT ( 'NONE',  ( 0.000000000000000000, 0.000000000000000000, 5.000000000000000000 ) ) ;
#73631=ORIENTED_EDGE ( 'NONE', *, *, #126516, .F. ) ;
#73632=ORIENTED_EDGE ( 'NONE', *, *, #68145, .F. ) ;
#73634=ORIENTED_EDGE ( 'NONE', *, *, #132303, .F. ) ;
#73635=DIRECTION ( 'NONE',  ( -0.7071067811865486830, -0.7071067811865464625, -0.000000000000000000 ) ) ;
#73636=DIRECTION ( 'NONE',  ( -0.7071067811865487940, 0.7071067811865463515, -0.000000000000000000 ) ) ;
#73637=DIRECTION ( 'NONE',  ( 0.7071067811865486830, -0.7071067811865464625, -0.000000000000000000 ) ) ;
#73638=CARTESIAN_POINT ( 'NONE',  ( 0.000000000000000000, 0.000000000000000000, 5.000000000000000000 ) ) ;
#73640=CARTESIAN_POINT ( 'NONE',  ( 28.49999999999980460, 15.05218569542901186, 5.000000000000000000 ) ) ;
#73641=ADVANCED_FACE ( 'NONE', ( #116749 ), #73970, .T. ) ;
#73643=CARTESIAN_POINT ( 'NONE',  ( -2.999999999999980016, -16.60178936734448740, 0.8616154019347429527 ) ) ;
#73644=LINE ( 'NONE', #138913, #79152 ) ;
#73645=ADVANCED_FACE ( 'NONE', ( #92849 ), #28334, .F. ) ;
#73648=CARTESIAN_POINT ( 'NONE',  ( -2.994519915287485734, 28.92564299267940342, 4.000000000000000000 ) ) ;
#73649=LINE ( 'NONE', #62794, #3585 ) ;
#73651=AXIS2_PLACEMENT_3D ( 'NONE', #35123, #134424, #35851 ) ;
#73652=EDGE_CURVE ( 'NONE', #78474, #24379, #15967, .T. ) ;
#73653=LINE ( 'NONE', #138194, #108609 ) ;
#73654=DIRECTION ( 'NONE',  ( -0.7071067811865486830, -0.7071067811865464625, 0.000000000000000000 ) ) ;
#73655=ORIENTED_EDGE ( 'NONE', *, *, #136972, .T. ) ;
#73656=AXIS2_PLACEMENT_3D ( 'NONE', #93161, #140243, #5407 ) ;
#73657=CARTESIAN_POINT ( 'NONE',  ( -5.816011393731002066, 28.73617430169783304, 5.000000000000000000 ) ) ;
#73658=DIRECTION ( 'NONE',  ( -0.7071067811865486830, -0.7071067811865464625, 0.000000000000000000 ) ) ;
#73659=ORIENTED_EDGE ( 'NONE', *, *, #70651, .T. ) ;
#73660=ORIENTED_EDGE ( 'NONE', *, *, #142685, .F. ) ;
#73661=LINE ( 'NONE', #106983, #2331 ) ;
#73664=VECTOR ( 'NONE', #51468, 1000.000000000000000 ) ;
#73665=LINE ( 'NONE', #128062, #15155 ) ;
#73667=DIRECTION ( 'NONE',  ( 0.7071067811865487940, 0.7071067811865463515, 0.000000000000000000 ) ) ;
#73668=VERTEX_POINT ( 'NONE', #137085 ) ;
#73669=EDGE_CURVE ( 'NONE', #94920, #117172, #60260, .T. ) ;
#73671=DIRECTION ( 'NONE',  ( -0.7071067811865487940, 0.7071067811865463515, -0.000000000000000000 ) ) ;
#73672=CARTESIAN_POINT ( 'NONE',  ( 13.84116387061258457, 6.089959206779446355, 4.000000000000000000 ) ) ;
#73673=CARTESIAN_POINT ( 'NONE',  ( 34.92499999999998295, 22.22500000000000142, 4.000000000000000000 ) ) ;
#73674=EDGE_LOOP ( 'NONE', ( #80598, #127535, #84168, #136888 ) ) ;
#73675=EDGE_CURVE ( 'NONE', #16867, #15871, #50788, .T. ) ;
#73676=DIRECTION ( 'NONE',  ( -0.000000000000000000, 0.3543493200069153248, 0.9351131265310292928 ) ) ;
#73677=EDGE_LOOP ( 'NONE', ( #32042, #70527, #111032, #71310 ) ) ;
#73679=DIRECTION ( 'NONE',  ( -0.7071067811865486830, -0.7071067811865464625, -0.000000000000000000 ) ) ;
#73680=CARTESIAN_POINT ( 'NONE',  ( -14.99999999999989519, -19.22509904557637839, 1.855685503482144227 ) ) ;
#73681=ORIENTED_EDGE ( 'NONE', *, *, #9676, .T. ) ;
#73682=DIRECTION ( 'NONE',  ( -0.000000000000000000, 0.000000000000000000, 1.000000000000000000 ) ) ;
#73684=DIRECTION ( 'NONE',  ( -0.7071067811865486830, -0.7071067811865464625, 0.000000000000000000 ) ) ;
#73686=EDGE_CURVE ( 'NONE', #13854, #70323, #39944, .T. ) ;
#73687=DIRECTION ( 'NONE',  ( -0.7071067811865487940, 0.7071067811865463515, 0.000000000000000000 ) ) ;
#73688=VERTEX_POINT ( 'NONE', #49396 ) ;
#73689=LINE ( 'NONE', #41057, #129651 ) ;
#73690=VECTOR ( 'NONE', #43451, 1000.000000000000227 ) ;
#73691=CARTESIAN_POINT ( 'NONE',  ( -17.99451991528748351, 28.92564299267950645, 4.000000000000000000 ) ) ;
#73693=FACE_OUTER_BOUND ( 'NONE', #83324, .T. ) ;
#73694=VERTEX_POINT ( 'NONE', #65981 ) ;
#73695=EDGE_CURVE ( 'NONE', #29435, #122913, #129765, .T. ) ;
#73696=ORIENTED_EDGE ( 'NONE', *, *, #1089, .T. ) ;
#73699=DIRECTION ( 'NONE',  ( -0.7071067811865486830, -0.7071067811865464625, 0.000000000000000000 ) ) ;
#73703=AXIS2_PLACEMENT_3D ( 'NONE', #65227, #109410, #1339 ) ;
#73704=CARTESIAN_POINT ( 'NONE',  ( 30.48921356237309510, -27.52281430457076894, 5.000000000000000000 ) ) ;
#73705=CARTESIAN_POINT ( 'NONE',  ( 7.828169399223476432, 9.759292476615614831, 4.000000000000000000 ) ) ;
#73707=AXIS2_PLACEMENT_3D ( 'NONE', #71500, #70116, #104086 ) ;
#73709=DIRECTION ( 'NONE',  ( -0.6830127018922180770, -0.6830127018922204085, -0.2588190451025213501 ) ) ;
#73710=CARTESIAN_POINT ( 'NONE',  ( 24.29974487139158867, -27.71228299555223273, 4.000000000000000000 ) ) ;
#73711=CARTESIAN_POINT ( 'NONE',  ( 19.49999999999985789, -2.777013188829488666, 4.549262955118046570 ) ) ;
#73712=VERTEX_POINT ( 'NONE', #55080 ) ;
#73713=ORIENTED_EDGE ( 'NONE', *, *, #107455, .T. ) ;
#73715=DIRECTION ( 'NONE',  ( -0.7071067811865486830, 0.7071067811865464625, 0.000000000000000000 ) ) ;
#73716=CARTESIAN_POINT ( 'NONE',  ( -25.49999999999982947, -1.592773361805396970, -6.492772025301170480 ) ) ;
#73717=CARTESIAN_POINT ( 'NONE',  ( 21.18398860626899349, 28.73617430169802134, 5.000000000000000000 ) ) ;
#73719=DIRECTION ( 'NONE',  ( 2.781805975412905890E-17, -0.3543493200069152693, 0.9351131265310292928 ) ) ;
#73721=ORIENTED_EDGE ( 'NONE', *, *, #29534, .T. ) ;
#73722=ORIENTED_EDGE ( 'NONE', *, *, #139595, .F. ) ;
#73723=ORIENTED_EDGE ( 'NONE', *, *, #104776, .T. ) ;
#73724=ORIENTED_EDGE ( 'NONE', *, *, #96607, .T. ) ;
#73725=CARTESIAN_POINT ( 'NONE',  ( 3.792893218813436551, 3.759292476615678336, 5.000000000000000000 ) ) ;
#73726=LINE ( 'NONE', #5593, #140387 ) ;
#73728=VERTEX_POINT ( 'NONE', #52892 ) ;
#73730=CARTESIAN_POINT ( 'NONE',  ( 4.566871997512545356, -21.74070752338406365, 6.915939825044062239 ) ) ;
#73732=EDGE_CURVE ( 'NONE', #56677, #103133, #31188, .T. ) ;
#73733=LINE ( 'NONE', #62889, #97077 ) ;
#73735=AXIS2_PLACEMENT_3D ( 'NONE', #103536, #57241, #89823 ) ;
#73737=EDGE_LOOP ( 'NONE', ( #99109, #35301, #44538, #73608 ) ) ;
#73738=CARTESIAN_POINT ( 'NONE',  ( -32.99999999999976552, -0.03360074219774071558, 5.000000000000000000 ) ) ;
#73741=ORIENTED_EDGE ( 'NONE', *, *, #38123, .T. ) ;
#73742=CARTESIAN_POINT ( 'NONE',  ( 11.99999999999992006, -2.904428200921297609, -6.989807076074969316 ) ) ;
#73743=ORIENTED_EDGE ( 'NONE', *, *, #131504, .T. ) ;
#73744=VECTOR ( 'NONE', #4027, 1000.000000000000000 ) ;
#73748=VERTEX_POINT ( 'NONE', #108691 ) ;
#73750=EDGE_LOOP ( 'NONE', ( #71981, #123499, #4003, #28811 ) ) ;
#73751=ORIENTED_EDGE ( 'NONE', *, *, #109920, .T. ) ;
#73753=EDGE_CURVE ( 'NONE', #126258, #31605, #101680, .T. ) ;
#73755=CARTESIAN_POINT ( 'NONE',  ( -8.994519915287490619, 28.92564299267944250, 4.000000000000000000 ) ) ;
#73756=CARTESIAN_POINT ( 'NONE',  ( -9.489213562373095101, -27.52281430457062328, 5.000000000000000000 ) ) ;
#73757=EDGE_CURVE ( 'NONE', #135458, #98615, #63121, .T. ) ;
#73759=DIRECTION ( 'NONE',  ( 1.000000000000000000, 0.000000000000000000, 0.000000000000000000 ) ) ;
#73760=EDGE_CURVE ( 'NONE', #26437, #139716, #130509, .T. ) ;
#73761=PLANE ( 'NONE',  #102279 ) ;
#73763=CARTESIAN_POINT ( 'NONE',  ( -12.78162688292485605, 21.74787736706806385, 4.999607392498049308 ) ) ;
#73765=EDGE_CURVE ( 'NONE', #123337, #64814, #30467, .T. ) ;
#73767=CARTESIAN_POINT ( 'NONE',  ( 35.52487387214932113, 14.25929247661557220, 9.797011795316720395 ) ) ;
#73768=DIRECTION ( 'NONE',  ( -0.7071067811865486830, -0.7071067811865464625, 0.000000000000000000 ) ) ;
#73769=EDGE_CURVE ( 'NONE', #71410, #7557, #74707, .T. ) ;
#73771=VECTOR ( 'NONE', #24968, 1000.000000000000000 ) ;
#73772=DIRECTION ( 'NONE',  ( 1.000000000000000000, 0.000000000000000000, 0.000000000000000000 ) ) ;
#73773=VERTEX_POINT ( 'NONE', #98564 ) ;
#73774=ORIENTED_EDGE ( 'NONE', *, *, #132289, .T. ) ;
#73775=ORIENTED_EDGE ( 'NONE', *, *, #52204, .T. ) ;
#73778=VECTOR ( 'NONE', #45848, 999.9999999999998863 ) ;
#73780=CARTESIAN_POINT ( 'NONE',  ( -0.7928932188134476533, -5.240707523384234179, 5.000000000000000000 ) ) ;
#73781=EDGE_CURVE ( 'NONE', #138304, #99771, #43482, .T. ) ;
#73784=VERTEX_POINT ( 'NONE', #7967 ) ;
#73788=EDGE_CURVE ( 'NONE', #86643, #398, #90407, .T. ) ;
#73791=CARTESIAN_POINT ( 'NONE',  ( 34.75611968250419181, -15.18706574529245046, 4.955485411084878500 ) ) ;
#73792=FACE_OUTER_BOUND ( 'NONE', #137552, .T. ) ;
#73793=DIRECTION ( 'NONE',  ( -0.7071067811865487940, 0.7071067811865463515, 0.000000000000000000 ) ) ;
#73794=EDGE_LOOP ( 'NONE', ( #80844, #45383, #141705, #73415 ) ) ;
#73795=EDGE_LOOP ( 'NONE', ( #12958, #13770, #136001, #103801 ) ) ;
#73796=ORIENTED_EDGE ( 'NONE', *, *, #12866, .F. ) ;
#73797=CARTESIAN_POINT ( 'NONE',  ( -54.29974487139159578, -27.71228299555243879, 4.000000000000000000 ) ) ;
#73798=CARTESIAN_POINT ( 'NONE',  ( 0.000000000000000000, 0.000000000000000000, 5.000000000000000000 ) ) ;
#73799=CARTESIAN_POINT ( 'NONE',  ( -5.292893218813416567, -0.7407075233842753681, 5.000000000000000000 ) ) ;
#73800=VECTOR ( 'NONE', #25648, 1000.000000000000000 ) ;
#73801=CARTESIAN_POINT ( 'NONE',  ( 3.707106781186525257, 2.259292476615692546, 5.000000000000000000 ) ) ;
#73802=CARTESIAN_POINT ( 'NONE',  ( -6.005480084712508493, 28.92564299267933947, 4.000000000000000000 ) ) ;
#73803=FACE_OUTER_BOUND ( 'NONE', #29943, .T. ) ;
#73804=CARTESIAN_POINT ( 'NONE',  ( 10.58990935480161610, 9.759292476615618384, 11.28811694763781226 ) ) ;
#73805=ADVANCED_FACE ( 'NONE', ( #121729 ), #76111, .T. ) ;
#73806=CARTESIAN_POINT ( 'NONE',  ( -31.49999999999977973, 9.431123077392092213, 4.000000000000000000 ) ) ;
#73808=CARTESIAN_POINT ( 'NONE',  ( -12.71230993966019618, -21.73547319004781642, 4.999917730833664642 ) ) ;
#73810=ADVANCED_FACE ( 'NONE', ( #143493 ), #52208, .F. ) ;
#73812=CARTESIAN_POINT ( 'NONE',  ( -31.49999999999977973, -15.29013452822857388, 0.3645803511609629344 ) ) ;
#73813=CARTESIAN_POINT ( 'NONE',  ( -13.83673880763391217, -22.22500000000000142, -2.991130486387429510 ) ) ;
#73814=EDGE_LOOP ( 'NONE', ( #96309, #21666, #122468, #45573 ) ) ;
#73815=ADVANCED_FACE ( 'NONE', ( #118888 ), #19577, .F. ) ;
#73817=FACE_OUTER_BOUND ( 'NONE', #97585, .T. ) ;
#73818=ORIENTED_EDGE ( 'NONE', *, *, #15510, .F. ) ;
#73819=DIRECTION ( 'NONE',  ( 0.7071067811865486830, -0.7071067811865464625, -0.000000000000000000 ) ) ;
#73820=CARTESIAN_POINT ( 'NONE',  ( -59.99451991528749772, 28.92564299267980132, 4.000000000000000000 ) ) ;
#73821=EDGE_LOOP ( 'NONE', ( #115691, #5809, #35528, #132040 ) ) ;
#73822=CARTESIAN_POINT ( 'NONE',  ( 5.293876922608006019, 22.22500000000000142, 4.000000000000000000 ) ) ;
#73824=VERTEX_POINT ( 'NONE', #36866 ) ;
#73827=DIRECTION ( 'NONE',  ( -0.000000000000000000, 0.3543493200069153248, 0.9351131265310292928 ) ) ;
#73828=PLANE ( 'NONE',  #108393 ) ;
#73829=ADVANCED_FACE ( 'NONE', ( #58698 ), #91295, .F. ) ;
#73832=DIRECTION ( 'NONE',  ( 0.7071067811865487940, 0.7071067811865463515, -0.000000000000000000 ) ) ;
#73835=CARTESIAN_POINT ( 'NONE',  ( 10.17183060077640100, 21.75929247661550647, 4.000000000000000000 ) ) ;
#73836=DIRECTION ( 'NONE',  ( -0.6830127018922180770, -0.6830127018922204085, -0.2588190451025213501 ) ) ;
#73837=ORIENTED_EDGE ( 'NONE', *, *, #48164, .T. ) ;
#73838=ORIENTED_EDGE ( 'NONE', *, *, #88418, .T. ) ;
#73840=CARTESIAN_POINT ( 'NONE',  ( -72.29974487139158157, -27.71228299555256669, 4.000000000000000000 ) ) ;
#73842=EDGE_CURVE ( 'NONE', #68263, #113749, #14417, .T. ) ;
#73843=CARTESIAN_POINT ( 'NONE',  ( -8.999999999999932498, -13.44781430457069504, 5.000000000000000000 ) ) ;
#73844=CARTESIAN_POINT ( 'NONE',  ( 0.7928932188134442116, 12.75929247661559529, 5.000000000000000000 ) ) ;
#73848=ORIENTED_EDGE ( 'NONE', *, *, #74720, .T. ) ;
#73849=VECTOR ( 'NONE', #59848, 1000.000000000000227 ) ;
#73850=VECTOR ( 'NONE', #133194, 1000.000000000000227 ) ;
#73851=VECTOR ( 'NONE', #32338, 999.9999999999998863 ) ;
#73853=VECTOR ( 'NONE', #94923, 999.9999999999998863 ) ;
#73854=CARTESIAN_POINT ( 'NONE',  ( 29.20666063542132207, 21.75929247661549581, 4.998822639870703632 ) ) ;
#73855=LINE ( 'NONE', #85418, #125248 ) ;
#73857=CARTESIAN_POINT ( 'NONE',  ( 3.289788898235945780, -22.22500000000000142, 19.48101205736676889 ) ) ;
#73858=CARTESIAN_POINT ( 'NONE',  ( -24.18398860626899705, 28.73617430169804265, 5.000000000000000000 ) ) ;
#73859=ORIENTED_EDGE ( 'NONE', *, *, #107376, .T. ) ;
#73860=DIRECTION ( 'NONE',  ( 1.000000000000000000, 0.000000000000000000, 0.000000000000000000 ) ) ;
#73862=CARTESIAN_POINT ( 'NONE',  ( 24.18398860626899705, 28.73617430169804265, 5.000000000000000000 ) ) ;
#73863=CARTESIAN_POINT ( 'NONE',  ( 7.499999999999950262, 18.05218569542898877, 5.000000000000000000 ) ) ;
#73864=LINE ( 'NONE', #118037, #121661 ) ;
#73865=CARTESIAN_POINT ( 'NONE',  ( -78.18398860626899705, 28.73617430169841924, 5.000000000000000000 ) ) ;
#73866=EDGE_LOOP ( 'NONE', ( #135526, #20759, #26090, #142750 ) ) ;
#73867=VERTEX_POINT ( 'NONE', #135499 ) ;
#73869=( BOUNDED_CURVE ( )  B_SPLINE_CURVE ( 3, ( #55741, #91241, #609, #124551 ),
 .UNSPECIFIED., .F., .T. ) 
 B_SPLINE_CURVE_WITH_KNOTS ( ( 4, 4 ),
 ( 5.106027341939269881, 6.645403452391244414 ),
 .UNSPECIFIED. ) 
 CURVE ( )  GEOMETRIC_REPRESENTATION_ITEM ( )  RATIONAL_B_SPLINE_CURVE ( ( 1.000000000000000000, 0.8120851936182256203, 0.8120851936182256203, 1.000000000000000000 ) ) 
 REPRESENTATION_ITEM ( '' )  );
#73870=ORIENTED_EDGE ( 'NONE', *, *, #43692, .T. ) ;
#73872=VECTOR ( 'NONE', #107323, 999.9999999999998863 ) ;
#73874=ORIENTED_EDGE ( 'NONE', *, *, #86436, .F. ) ;
#73875=DIRECTION ( 'NONE',  ( 0.7071067811865487940, 0.7071067811865463515, -0.000000000000000000 ) ) ;
#73877=ADVANCED_FACE ( 'NONE', ( #89824 ), #134067, .F. ) ;
#73878=VECTOR ( 'NONE', #105389, 999.9999999999998863 ) ;
#73880=EDGE_CURVE ( 'NONE', #41017, #54692, #13668, .T. ) ;
#73881=ORIENTED_EDGE ( 'NONE', *, *, #28888, .F. ) ;
#73882=FACE_OUTER_BOUND ( 'NONE', #4351, .T. ) ;
#73883=ORIENTED_EDGE ( 'NONE', *, *, #43906, .F. ) ;
#73884=CARTESIAN_POINT ( 'NONE',  ( 12.48921356237309155, -27.52281430457064104, 5.000000000000000000 ) ) ;
#73885=CARTESIAN_POINT ( 'NONE',  ( -75.48921356237309510, -27.52281430457107803, 5.000000000000000000 ) ) ;
#73886=VECTOR ( 'NONE', #37330, 1000.000000000000000 ) ;
#73887=CARTESIAN_POINT ( 'NONE',  ( 75.18398860626899705, 28.73617430169839793, 5.000000000000000000 ) ) ;
#73892=FACE_OUTER_BOUND ( 'NONE', #131772, .T. ) ;
#73893=ADVANCED_FACE ( 'NONE', ( #12966 ), #34755, .F. ) ;
#73894=LINE ( 'NONE', #106474, #10583 ) ;
#73896=VECTOR ( 'NONE', #30149, 1000.000000000000000 ) ;
#73899=ORIENTED_EDGE ( 'NONE', *, *, #17194, .F. ) ;
#73900=ORIENTED_EDGE ( 'NONE', *, *, #117140, .T. ) ;
#73901=FACE_OUTER_BOUND ( 'NONE', #106050, .T. ) ;
#73902=ORIENTED_EDGE ( 'NONE', *, *, #107225, .F. ) ;
#73903=EDGE_LOOP ( 'NONE', ( #126450, #50658, #90927, #90763 ) ) ;
#73904=VECTOR ( 'NONE', #111030, 999.9999999999998863 ) ;
#73906=CARTESIAN_POINT ( 'NONE',  ( 4.499999999999979572, 4.466399257802216027, 5.000000000000000000 ) ) ;
#73907=ORIENTED_EDGE ( 'NONE', *, *, #95673, .F. ) ;
#73909=ADVANCED_FACE ( 'NONE', ( #57242 ), #2067, .T. ) ;
#73910=DIRECTION ( 'NONE',  ( 0.7071067811865487940, 0.7071067811865463515, 0.000000000000000000 ) ) ;
#73911=CARTESIAN_POINT ( 'NONE',  ( -23.29289321881329045, 14.25929247661557042, 5.000000000000000000 ) ) ;
#73913=ORIENTED_EDGE ( 'NONE', *, *, #94539, .T. ) ;
#73914=CARTESIAN_POINT ( 'NONE',  ( 33.29974487139158867, -27.71228299555229313, 4.000000000000000000 ) ) ;
#73915=PLANE ( 'NONE',  #70862 ) ;
#73916=ORIENTED_EDGE ( 'NONE', *, *, #124857, .T. ) ;
#73917=FACE_OUTER_BOUND ( 'NONE', #112356, .T. ) ;
#73918=FACE_OUTER_BOUND ( 'NONE', #96810, .T. ) ;
#73919=CARTESIAN_POINT ( 'NONE',  ( -25.49999999999982236, -13.53360074219759746, 5.000000000000000000 ) ) ;
#73920=EDGE_CURVE ( 'NONE', #93975, #126820, #131319, .T. ) ;
#73921=VERTEX_POINT ( 'NONE', #66670 ) ;
#73924=EDGE_LOOP ( 'NONE', ( #84797, #95183, #60703, #138525 ) ) ;
#73925=VERTEX_POINT ( 'NONE', #46379 ) ;
#73927=ADVANCED_FACE ( 'NONE', ( #79731 ), #68827, .F. ) ;
#73929=DIRECTION ( 'NONE',  ( -0.7071067811865487940, 0.7071067811865463515, 0.000000000000000000 ) ) ;
#73930=CARTESIAN_POINT ( 'NONE',  ( 42.18398860626899705, 28.73617430169816700, 5.000000000000000000 ) ) ;
#73931=EDGE_CURVE ( 'NONE', #6272, #122150, #25278, .T. ) ;
#73932=DIRECTION ( 'NONE',  ( -0.7071067811865487940, 0.7071067811865463515, 0.000000000000000000 ) ) ;
#73933=EDGE_CURVE ( 'NONE', #141351, #6455, #55804, .T. ) ;
#73934=DIRECTION ( 'NONE',  ( 0.6830127018922181881, 0.6830127018922202975, -0.2588190451025214056 ) ) ;
#73935=LINE ( 'NONE', #118112, #36627 ) ;
#73936=EDGE_CURVE ( 'NONE', #126961, #68281, #100007, .T. ) ;
#73937=PLANE ( 'NONE',  #111737 ) ;
#73938=LINE ( 'NONE', #74677, #22726 ) ;
#73939=DIRECTION ( 'NONE',  ( -0.000000000000000000, 0.3543493200069153248, 0.9351131265310292928 ) ) ;
#73942=ORIENTED_EDGE ( 'NONE', *, *, #51404, .T. ) ;
#73943=VERTEX_POINT ( 'NONE', #49211 ) ;
#73944=ORIENTED_EDGE ( 'NONE', *, *, #117786, .F. ) ;
#73946=CARTESIAN_POINT ( 'NONE',  ( 31.49999999999978684, -8.947814304570730570, 5.000000000000000000 ) ) ;
#73948=VECTOR ( 'NONE', #14059, 1000.000000000000227 ) ;
#73950=CIRCLE ( 'NONE', #80895, 0.5000000000000004441 ) ;
#73951=VECTOR ( 'NONE', #117213, 1000.000000000000114 ) ;
#73952=ORIENTED_EDGE ( 'NONE', *, *, #69714, .F. ) ;
#73953=PLANE ( 'NONE',  #118559 ) ;
#73954=CARTESIAN_POINT ( 'NONE',  ( 60.18398860626900415, 28.73617430169829490, 5.000000000000000000 ) ) ;
#73955=EDGE_CURVE ( 'NONE', #80026, #94676, #106374, .T. ) ;
#73956=EDGE_CURVE ( 'NONE', #59180, #1974, #40474, .T. ) ;
#73957=CARTESIAN_POINT ( 'NONE',  ( 32.20710678118632586, 18.75929247661552424, 5.000000000000000000 ) ) ;
#73958=EDGE_LOOP ( 'NONE', ( #122550, #102346, #6604 ) ) ;
#73959=CARTESIAN_POINT ( 'NONE',  ( 2.999999999999975131, -7.068876922607738145, 4.000000000000000000 ) ) ;
#73960=VECTOR ( 'NONE', #22438, 1000.000000000000227 ) ;
#73962=ADVANCED_FACE ( 'NONE', ( #71661 ), #81854, .F. ) ;
#73963=DIRECTION ( 'NONE',  ( -0.7071067811865486830, -0.7071067811865464625, -0.000000000000000000 ) ) ;
#73964=DIRECTION ( 'NONE',  ( 0.000000000000000000, 0.000000000000000000, -1.000000000000000000 ) ) ;
#73966=EDGE_LOOP ( 'NONE', ( #1217, #140637, #40135, #87998 ) ) ;
#73968=CARTESIAN_POINT ( 'NONE',  ( -59.99451991528749772, 28.92564299267980132, 4.000000000000000000 ) ) ;
#73969=CARTESIAN_POINT ( 'NONE',  ( -36.48921356237310221, -27.52281430457080802, 5.000000000000000000 ) ) ;
#73970=PLANE ( 'NONE',  #141509 ) ;
#73971=VERTEX_POINT ( 'NONE', #105675 ) ;
#73972=ORIENTED_EDGE ( 'NONE', *, *, #83420, .T. ) ;
#73974=ORIENTED_EDGE ( 'NONE', *, *, #122041, .F. ) ;
#73975=DIRECTION ( 'NONE',  ( -0.6830127018922180770, -0.6830127018922204085, -0.2588190451025213501 ) ) ;
#73976=VECTOR ( 'NONE', #47460, 1000.000000000000000 ) ;
#73978=CARTESIAN_POINT ( 'NONE',  ( -34.42500000000001137, -13.45860074219784863, 5.000000000000000000 ) ) ;
#73979=CARTESIAN_POINT ( 'NONE',  ( -26.99999999999980815, -4.068876922607768343, 4.000000000000000000 ) ) ;
#73980=VERTEX_POINT ( 'NONE', #7057 ) ;
#73981=PLANE ( 'NONE',  #11394 ) ;
#73983=DIRECTION ( 'NONE',  ( -0.7071067811865487940, 0.7071067811865463515, -0.000000000000000000 ) ) ;
#73984=FACE_OUTER_BOUND ( 'NONE', #104349, .T. ) ;
#73985=ADVANCED_FACE ( 'NONE', ( #115827 ), #137640, .F. ) ;
#73986=VERTEX_POINT ( 'NONE', #138340 ) ;
#73987=CARTESIAN_POINT ( 'NONE',  ( 0.000000000000000000, 0.000000000000000000, 5.000000000000000000 ) ) ;
#73988=AXIS2_PLACEMENT_3D ( 'NONE', #5912, #72693, #114003 ) ;
#73989=DIRECTION ( 'NONE',  ( -0.7071067811865486830, -0.7071067811865464625, 0.000000000000000000 ) ) ;
#73990=ORIENTED_EDGE ( 'NONE', *, *, #138720, .F. ) ;
#73991=AXIS2_PLACEMENT_3D ( 'NONE', #110518, #132336, #56216 ) ;
#73992=DIRECTION ( 'NONE',  ( -0.000000000000000000, 0.3543493200069153248, 0.9351131265310292928 ) ) ;
#73993=ORIENTED_EDGE ( 'NONE', *, *, #24952, .T. ) ;
#73994=ORIENTED_EDGE ( 'NONE', *, *, #110496, .F. ) ;
#73995=AXIS2_PLACEMENT_3D ( 'NONE', #16057, #6600, #104534 ) ;
#73996=CARTESIAN_POINT ( 'NONE',  ( 5.999999999999960032, 11.96639925780213964, 5.000000000000000000 ) ) ;
#73997=AXIS2_PLACEMENT_3D ( 'NONE', #20510, #87231, #74216 ) ;
#73998=PLANE ( 'NONE',  #15973 ) ;
#73999=ORIENTED_EDGE ( 'NONE', *, *, #112961, .F. ) ;
#74001=EDGE_CURVE ( 'NONE', #103751, #123300, #59382, .T. ) ;
#74002=PLANE ( 'NONE',  #49863 ) ;
#74003=CARTESIAN_POINT ( 'NONE',  ( 28.49999999999980105, 19.39370406404969671, 1.459788787078136307 ) ) ;
#74004=DIRECTION ( 'NONE',  ( -0.7071067811865487940, 0.7071067811865463515, 0.000000000000000000 ) ) ;
#74006=EDGE_CURVE ( 'NONE', #91203, #6385, #5650, .T. ) ;
#74009=LINE ( 'NONE', #8005, #125294 ) ;
#74010=LINE ( 'NONE', #21031, #36411 ) ;
#74012=LINE ( 'NONE', #71893, #18844 ) ;
#74013=LINE ( 'NONE', #142834, #13623 ) ;
#74014=CARTESIAN_POINT ( 'NONE',  ( 17.12514619309224173, -14.24070752338413293, 9.401115078912619438 ) ) ;
#74015=CARTESIAN_POINT ( 'NONE',  ( 11.99999999999992717, -4.447814304570779420, 5.000000000000000000 ) ) ;
#74016=VERTEX_POINT ( 'NONE', #94797 ) ;
#74018=ORIENTED_EDGE ( 'NONE', *, *, #120169, .T. ) ;
#74021=VERTEX_POINT ( 'NONE', #39762 ) ;
#74022=ADVANCED_FACE ( 'NONE', ( #51339 ), #4177, .F. ) ;
#74024=CARTESIAN_POINT ( 'NONE',  ( 0.000000000000000000, 0.000000000000000000, 5.000000000000000000 ) ) ;
#74025=CARTESIAN_POINT ( 'NONE',  ( 34.92382263987068569, 21.75929247661549937, 4.252424926123345550 ) ) ;
#74026=ORIENTED_EDGE ( 'NONE', *, *, #100282, .T. ) ;
#74027=LINE ( 'NONE', #117494, #53165 ) ;
#74028=DIRECTION ( 'NONE',  ( -0.3543493200069162685, -0.000000000000000000, -0.9351131265310288487 ) ) ;
#74030=LINE ( 'NONE', #72648, #120666 ) ;
#74033=EDGE_LOOP ( 'NONE', ( #72252, #7385, #108218, #39272, #89552 ) ) ;
#74034=DIRECTION ( 'NONE',  ( -0.7071067811865487940, 0.7071067811865463515, -0.000000000000000000 ) ) ;
#74035=DIRECTION ( 'NONE',  ( 0.7071067811865486830, -0.7071067811865464625, -0.000000000000000000 ) ) ;
#74037=DIRECTION ( 'NONE',  ( -0.7071067811865486830, 0.7071067811865464625, 0.000000000000000000 ) ) ;
#74039=DIRECTION ( 'NONE',  ( 1.000000000000000000, 0.000000000000000000, 0.000000000000000000 ) ) ;
#74040=CARTESIAN_POINT ( 'NONE',  ( -18.48921356237309510, -27.52281430457068367, 5.000000000000000000 ) ) ;
#74041=CARTESIAN_POINT ( 'NONE',  ( -32.99999999999976552, -7.447814304570749222, 5.000000000000000000 ) ) ;
#74042=VERTEX_POINT ( 'NONE', #99081 ) ;
#74045=ORIENTED_EDGE ( 'NONE', *, *, #92402, .T. ) ;
#74046=LINE ( 'NONE', #31966, #37038 ) ;
#74047=LINE ( 'NONE', #21077, #124205 ) ;
#74049=CARTESIAN_POINT ( 'NONE',  ( 57.18398860626899705, 28.73617430169827358, 5.000000000000000000 ) ) ;
#74051=DIRECTION ( 'NONE',  ( 1.000000000000000000, 0.000000000000000000, 0.000000000000000000 ) ) ;
#74053=EDGE_CURVE ( 'NONE', #53831, #27000, #53470, .T. ) ;
#74054=EDGE_LOOP ( 'NONE', ( #67176, #58871, #37466, #1967 ) ) ;
#74055=LINE ( 'NONE', #16818, #20146 ) ;
#74056=VERTEX_POINT ( 'NONE', #32437 ) ;
#74057=PLANE ( 'NONE',  #48537 ) ;
#74058=VECTOR ( 'NONE', #107456, 999.9999999999998863 ) ;
#74059=VECTOR ( 'NONE', #123743, 1000.000000000000000 ) ;
#74060=VECTOR ( 'NONE', #89302, 1000.000000000000000 ) ;
#74061=DIRECTION ( 'NONE',  ( -0.7071067811865487940, 0.7071067811865463515, -0.000000000000000000 ) ) ;
#74063=VECTOR ( 'NONE', #74119, 999.9999999999998863 ) ;
#74064=CARTESIAN_POINT ( 'NONE',  ( 30.29974487139158867, -27.71228299555227537, 4.000000000000000000 ) ) ;
#74065=VERTEX_POINT ( 'NONE', #120849 ) ;
#74067=ORIENTED_EDGE ( 'NONE', *, *, #51089, .F. ) ;
#74068=FACE_OUTER_BOUND ( 'NONE', #95153, .T. ) ;
#74069=EDGE_CURVE ( 'NONE', #9302, #63481, #128875, .T. ) ;
#74070=CARTESIAN_POINT ( 'NONE',  ( 44.99451991528749772, 28.92564299267969474, 4.000000000000000000 ) ) ;
#74071=PLANE ( 'NONE',  #115011 ) ;
#74072=LINE ( 'NONE', #100105, #29842 ) ;
#74076=ORIENTED_EDGE ( 'NONE', *, *, #14860, .F. ) ;
#74078=VERTEX_POINT ( 'NONE', #63658 ) ;
#74079=ORIENTED_EDGE ( 'NONE', *, *, #131313, .F. ) ;
#74081=AXIS2_PLACEMENT_3D ( 'NONE', #18239, #73394, #65390 ) ;
#74082=ORIENTED_EDGE ( 'NONE', *, *, #81182, .T. ) ;
#74084=VECTOR ( 'NONE', #43214, 999.9999999999998863 ) ;
#74085=CARTESIAN_POINT ( 'NONE',  ( -48.29974487139158867, -27.71228299555239971, 4.000000000000000000 ) ) ;
#74087=VERTEX_POINT ( 'NONE', #31716 ) ;
#74088=LINE ( 'NONE', #107416, #55230 ) ;
#74089=DIRECTION ( 'NONE',  ( -1.000000000000000000, 0.000000000000000000, 0.000000000000000000 ) ) ;
#74090=AXIS2_PLACEMENT_3D ( 'NONE', #3562, #45013, #123264 ) ;
#74091=DIRECTION ( 'NONE',  ( -0.7071067811865487940, 0.7071067811865463515, -0.000000000000000000 ) ) ;
#74092=FACE_BOUND ( 'NONE', #122694, .T. ) ;
#74093=ORIENTED_EDGE ( 'NONE', *, *, #41928, .T. ) ;
#74095=VECTOR ( 'NONE', #122594, 1000.000000000000227 ) ;
#74097=EDGE_LOOP ( 'NONE', ( #83081, #41400, #28749, #84318 ) ) ;
#74098=DIRECTION ( 'NONE',  ( 0.7071067811865487940, 0.7071067811865463515, 0.000000000000000000 ) ) ;
#74099=VERTEX_POINT ( 'NONE', #75936 ) ;
#74101=EDGE_LOOP ( 'NONE', ( #16724, #100724, #68651, #39590 ) ) ;
#74102=LINE ( 'NONE', #41453, #100343 ) ;
#74103=ORIENTED_EDGE ( 'NONE', *, *, #13327, .T. ) ;
#74106=ORIENTED_EDGE ( 'NONE', *, *, #57506, .F. ) ;
#74107=LINE ( 'NONE', #126338, #55675 ) ;
#74108=EDGE_CURVE ( 'NONE', #119037, #100881, #100585, .T. ) ;
#74109=DIRECTION ( 'NONE',  ( 0.7071067811865487940, 0.7071067811865463515, 0.000000000000000000 ) ) ;
#74110=ORIENTED_EDGE ( 'NONE', *, *, #45139, .F. ) ;
#74111=DIRECTION ( 'NONE',  ( 0.6830127018922180770, -0.6830127018922204085, -0.2588190451025213501 ) ) ;
#74112=AXIS2_PLACEMENT_3D ( 'NONE', #137146, #25503, #37850 ) ;
#74114=EDGE_CURVE ( 'NONE', #111086, #9245, #84671, .T. ) ;
#74115=PLANE ( 'NONE',  #27048 ) ;
#74117=DIRECTION ( 'NONE',  ( 0.3543493200069162685, -0.000000000000000000, -0.9351131265310288487 ) ) ;
#74118=LINE ( 'NONE', #140773, #135119 ) ;
#74119=DIRECTION ( 'NONE',  ( -0.7071067811865486830, -0.7071067811865464625, 0.000000000000000000 ) ) ;
#74120=ORIENTED_EDGE ( 'NONE', *, *, #118690, .T. ) ;
#74122=ORIENTED_EDGE ( 'NONE', *, *, #142380, .F. ) ;
#74123=DIRECTION ( 'NONE',  ( -0.7071067811865487940, 0.7071067811865463515, -0.000000000000000000 ) ) ;
#74125=ORIENTED_EDGE ( 'NONE', *, *, #24707, .F. ) ;
#74126=ORIENTED_EDGE ( 'NONE', *, *, #112885, .T. ) ;
#74127=VERTEX_POINT ( 'NONE', #7794 ) ;
#74128=CARTESIAN_POINT ( 'NONE',  ( 8.843876922607519120, -22.22500000000000497, 4.000000000000000000 ) ) ;
#74131=EDGE_CURVE ( 'NONE', #120155, #4917, #117964, .T. ) ;
#74132=CARTESIAN_POINT ( 'NONE',  ( 30.48921356237309510, -27.52281430457076894, 5.000000000000000000 ) ) ;
#74133=EDGE_LOOP ( 'NONE', ( #126072, #99380, #17586, #72972, #62383 ) ) ;
#74134=FACE_OUTER_BOUND ( 'NONE', #20673, .T. ) ;
#74135=EDGE_CURVE ( 'NONE', #82254, #3598, #120110, .T. ) ;
#74138=PLANE ( 'NONE',  #19481 ) ;
#74139=ORIENTED_EDGE ( 'NONE', *, *, #31383, .T. ) ;
#74141=CARTESIAN_POINT ( 'NONE',  ( -36.18398860626899705, 28.73617430169812437, 5.000000000000000000 ) ) ;
#74143=ADVANCED_FACE ( 'NONE', ( #41155 ), #85362, .F. ) ;
#74144=DIRECTION ( 'NONE',  ( 0.7071067811865486830, -0.7071067811865464625, -0.000000000000000000 ) ) ;
#74145=ORIENTED_EDGE ( 'NONE', *, *, #76119, .T. ) ;
#74146=DIRECTION ( 'NONE',  ( 0.7071067811865486830, -0.7071067811865464625, -0.000000000000000000 ) ) ;
#74148=DIRECTION ( 'NONE',  ( -0.3543493200069162685, -0.000000000000000000, -0.9351131265310288487 ) ) ;
#74149=CARTESIAN_POINT ( 'NONE',  ( 34.42499999999998295, 2.977185695429370504, 5.000000000000000000 ) ) ;
#74150=LINE ( 'NONE', #53846, #5534 ) ;
#74151=ORIENTED_EDGE ( 'NONE', *, *, #13058, .T. ) ;
#74152=VECTOR ( 'NONE', #19394, 1000.000000000000000 ) ;
#74153=DIRECTION ( 'NONE',  ( -1.000000000000000000, 0.000000000000000000, 0.000000000000000000 ) ) ;
#74154=DIRECTION ( 'NONE',  ( -0.7071067811865486830, -0.7071067811865464625, 0.000000000000000000 ) ) ;
#74155=CARTESIAN_POINT ( 'NONE',  ( -34.49999999999975842, 21.05432934483072671, 4.994342998332167660 ) ) ;
#74156=VECTOR ( 'NONE', #45217, 999.9999999999998863 ) ;
#74157=EDGE_CURVE ( 'NONE', #94079, #12165, #112146, .T. ) ;
#74158=VERTEX_POINT ( 'NONE', #67203 ) ;
#74161=AXIS2_PLACEMENT_3D ( 'NONE', #33366, #65986, #91300 ) ;
#74162=DIRECTION ( 'NONE',  ( 0.7071067811865487940, 0.7071067811865463515, -0.000000000000000000 ) ) ;
#74163=DIRECTION ( 'NONE',  ( 0.7071067811865487940, 0.7071067811865463515, -0.000000000000000000 ) ) ;
#74164=AXIS2_PLACEMENT_3D ( 'NONE', #41855, #141904, #20073 ) ;
#74165=CARTESIAN_POINT ( 'NONE',  ( -1.499999999999987566, -2.568876922607790103, 4.000000000000000000 ) ) ;
#74166=PLANE ( 'NONE',  #62334 ) ;
#74167=ORIENTED_EDGE ( 'NONE', *, *, #12075, .T. ) ;
#74168=ORIENTED_EDGE ( 'NONE', *, *, #58965, .T. ) ;
#74169=CARTESIAN_POINT ( 'NONE',  ( 19.73493329717937428, 12.75929247661558996, 18.34774599283951702 ) ) ;
#74170=VECTOR ( 'NONE', #82589, 1000.000000000000000 ) ;
#74172=ADVANCED_FACE ( 'NONE', ( #57781 ), #22937, .F. ) ;
#74174=CARTESIAN_POINT ( 'NONE',  ( -31.82816939922330945, 9.759292476615621936, 4.000000000000000000 ) ) ;
#74175=CARTESIAN_POINT ( 'NONE',  ( -18.32816939922339827, 14.25929247661557397, 4.000000000000000000 ) ) ;
#74176=ORIENTED_EDGE ( 'NONE', *, *, #98653, .T. ) ;
#74177=DIRECTION ( 'NONE',  ( -0.7071067811865487940, 0.7071067811865463515, 0.000000000000000000 ) ) ;
#74178=DIRECTION ( 'NONE',  ( -0.7071067811865486830, -0.7071067811865464625, -0.000000000000000000 ) ) ;
#74179=CARTESIAN_POINT ( 'NONE',  ( 10.17183060077640100, 6.759292476615647693, 4.000000000000000000 ) ) ;
#74180=VECTOR ( 'NONE', #13724, 1000.000000000000227 ) ;
#74181=CARTESIAN_POINT ( 'NONE',  ( -19.49999999999985434, -4.533600742197692490, 5.000000000000000000 ) ) ;
#74184=VECTOR ( 'NONE', #34463, 1000.000000000000227 ) ;
#74185=ORIENTED_EDGE ( 'NONE', *, *, #104747, .F. ) ;
#74186=CARTESIAN_POINT ( 'NONE',  ( 45.18398860626900415, 28.73617430169818832, 5.000000000000000000 ) ) ;
#74187=VECTOR ( 'NONE', #121858, 1000.000000000000000 ) ;
#74188=ORIENTED_EDGE ( 'NONE', *, *, #94046, .T. ) ;
#74189=EDGE_CURVE ( 'NONE', #42198, #40019, #12797, .T. ) ;
#74190=VECTOR ( 'NONE', #22108, 1000.000000000000000 ) ;
#74191=VERTEX_POINT ( 'NONE', #112834 ) ;
#74192=DIRECTION ( 'NONE',  ( -0.7071067811865487940, 0.7071067811865463515, -0.000000000000000000 ) ) ;
#74194=AXIS2_PLACEMENT_3D ( 'NONE', #140162, #8172, #52411 ) ;
#74195=DIRECTION ( 'NONE',  ( -0.6830127018922180770, -0.6830127018922204085, -0.2588190451025213501 ) ) ;
#74196=DIRECTION ( 'NONE',  ( -0.000000000000000000, -0.000000000000000000, 1.000000000000000000 ) ) ;
#74197=CARTESIAN_POINT ( 'NONE',  ( 22.17183060077632817, -11.24070752338416490, 4.000000000000000000 ) ) ;
#74198=CARTESIAN_POINT ( 'NONE',  ( -57.29974487139158157, -27.71228299555246011, 4.000000000000000000 ) ) ;
#74199=DIRECTION ( 'NONE',  ( -0.7071067811865487940, 0.7071067811865463515, 0.000000000000000000 ) ) ;
#74200=EDGE_CURVE ( 'NONE', #32877, #85323, #44028, .T. ) ;
#74201=VECTOR ( 'NONE', #80948, 1000.000000000000000 ) ;
#74202=EDGE_LOOP ( 'NONE', ( #17188, #77478, #91889, #142676 ) ) ;
#74203=DIRECTION ( 'NONE',  ( -0.000000000000000000, 0.3543493200069153248, 0.9351131265310292928 ) ) ;
#74204=DIRECTION ( 'NONE',  ( 0.6830127018922180770, -0.6830127018922204085, -0.2588190451025213501 ) ) ;
#74205=CARTESIAN_POINT ( 'NONE',  ( -8.999999999999934275, -16.60178936734449451, 0.8616154019347290749 ) ) ;
#74206=CARTESIAN_POINT ( 'NONE',  ( -34.92500000000001137, -15.18334561358941315, 4.500000000000000888 ) ) ;
#74207=LINE ( 'NONE', #52430, #45118 ) ;
#74208=DIRECTION ( 'NONE',  ( -0.7071067811865486830, -0.7071067811865464625, 0.000000000000000000 ) ) ;
#74210=DIRECTION ( 'NONE',  ( 1.000000000000000000, 0.000000000000000000, 0.000000000000000000 ) ) ;
#74212=ORIENTED_EDGE ( 'NONE', *, *, #44709, .F. ) ;
#74213=ORIENTED_EDGE ( 'NONE', *, *, #129035, .F. ) ;
#74215=FACE_OUTER_BOUND ( 'NONE', #3391, .T. ) ;
#74216=DIRECTION ( 'NONE',  ( 0.7071067811865487940, -0.7071067811865463515, 0.000000000000000000 ) ) ;
#74218=CARTESIAN_POINT ( 'NONE',  ( 60.18398860626900415, 28.73617430169829490, 5.000000000000000000 ) ) ;
#74222=EDGE_CURVE ( 'NONE', #55809, #111783, #101967, .T. ) ;
#74223=ORIENTED_EDGE ( 'NONE', *, *, #137527, .T. ) ;
#74225=ORIENTED_EDGE ( 'NONE', *, *, #10564, .F. ) ;
#74226=EDGE_LOOP ( 'NONE', ( #86441, #45868, #32641, #116498 ) ) ;
#74229=LINE ( 'NONE', #95253, #77816 ) ;
#74230=CARTESIAN_POINT ( 'NONE',  ( 6.299744871391586898, -27.71228299555210484, 4.000000000000000000 ) ) ;
#74231=PLANE ( 'NONE',  #138978 ) ;
#74232=ORIENTED_EDGE ( 'NONE', *, *, #17034, .T. ) ;
#74233=ADVANCED_FACE ( 'NONE', ( #80244 ), #88246, .F. ) ;
#74234=CARTESIAN_POINT ( 'NONE',  ( -60.48921356237309510, -27.52281430457097500, 5.000000000000000000 ) ) ;
#74235=PLANE ( 'NONE',  #19807 ) ;
#74236=ORIENTED_EDGE ( 'NONE', *, *, #142931, .F. ) ;
#74237=ADVANCED_FACE ( 'NONE', ( #78799 ), #56370, .F. ) ;
#74239=DIRECTION ( 'NONE',  ( 0.7071067811865486830, -0.7071067811865464625, -0.000000000000000000 ) ) ;
#74241=LINE ( 'NONE', #141647, #111169 ) ;
#74242=VECTOR ( 'NONE', #46045, 1000.000000000000000 ) ;
#74243=CARTESIAN_POINT ( 'NONE',  ( 9.005480084712511157, 28.92564299267931816, 4.000000000000000000 ) ) ;
#74244=EDGE_LOOP ( 'NONE', ( #108492, #134877, #39068, #128954 ) ) ;
#74245=EDGE_CURVE ( 'NONE', #137134, #38880, #135336, .T. ) ;
#74246=VERTEX_POINT ( 'NONE', #45479 ) ;
#74249=DIRECTION ( 'NONE',  ( 1.000000000000000000, 0.000000000000000000, 0.000000000000000000 ) ) ;
#74250=DIRECTION ( 'NONE',  ( 0.7071067811865487940, -0.7071067811865463515, 0.000000000000000000 ) ) ;
#74251=CARTESIAN_POINT ( 'NONE',  ( -5.994519915287488843, 28.92564299267942118, 4.000000000000000000 ) ) ;
#74252=VERTEX_POINT ( 'NONE', #46197 ) ;
#74253=ORIENTED_EDGE ( 'NONE', *, *, #113271, .F. ) ;
#74254=DIRECTION ( 'NONE',  ( -0.7071067811865486830, -0.7071067811865464625, 0.000000000000000000 ) ) ;
#74255=CARTESIAN_POINT ( 'NONE',  ( 17.39060256275758221, -2.561874075326514788, 4.636692559446315975 ) ) ;
#74256=VECTOR ( 'NONE', #126932, 1000.000000000000000 ) ;
#74257=ORIENTED_EDGE ( 'NONE', *, *, #92753, .F. ) ;
#74261=VERTEX_POINT ( 'NONE', #90371 ) ;
#74262=DIRECTION ( 'NONE',  ( 0.3543493200069162685, -0.000000000000000000, -0.9351131265310288487 ) ) ;
#74263=ORIENTED_EDGE ( 'NONE', *, *, #101737, .T. ) ;
#74264=CARTESIAN_POINT ( 'NONE',  ( 0.000000000000000000, 0.000000000000000000, 5.000000000000000000 ) ) ;
#74265=DIRECTION ( 'NONE',  ( -0.7071067811865487940, 0.7071067811865463515, -0.000000000000000000 ) ) ;
#74266=CIRCLE ( 'NONE', #109000, 5.968999999999998529 ) ;
#74267=AXIS2_PLACEMENT_3D ( 'NONE', #71687, #50634, #128211 ) ;
#74271=CARTESIAN_POINT ( 'NONE',  ( -6.489213562373093325, -27.52281430457059841, 5.000000000000000000 ) ) ;
#74272=FACE_BOUND ( 'NONE', #1790, .T. ) ;
#74273=CARTESIAN_POINT ( 'NONE',  ( 34.17183060077623225, -8.240707523384193323, 4.000000000000000000 ) ) ;
#74275=AXIS2_PLACEMENT_3D ( 'NONE', #72307, #70851, #103429 ) ;
#74278=VERTEX_POINT ( 'NONE', #44782 ) ;
#74281=EDGE_CURVE ( 'NONE', #6180, #98003, #24403, .T. ) ;
#74282=ORIENTED_EDGE ( 'NONE', *, *, #41640, .T. ) ;
#74284=ORIENTED_EDGE ( 'NONE', *, *, #102266, .T. ) ;
#74285=VECTOR ( 'NONE', #82835, 999.9999999999998863 ) ;
#74286=CARTESIAN_POINT ( 'NONE',  ( 31.49999999999977973, -16.91253812416059077, 4.000000000000000000 ) ) ;
#74287=EDGE_CURVE ( 'NONE', #120984, #20734, #22235, .T. ) ;
#74288=AXIS2_PLACEMENT_3D ( 'NONE', #120126, #96238, #77414 ) ;
#74289=CARTESIAN_POINT ( 'NONE',  ( 4.171830600776439191, -17.24070752338410628, 4.000000000000000000 ) ) ;
#74291=EDGE_CURVE ( 'NONE', #9775, #39717, #133886, .T. ) ;
#74293=DIRECTION ( 'NONE',  ( 0.6830127018922181881, 0.6830127018922202975, -0.2588190451025214056 ) ) ;
#74296=CARTESIAN_POINT ( 'NONE',  ( 11.99999999999991651, -15.41253812416059787, 4.000000000000000000 ) ) ;
#74300=DIRECTION ( 'NONE',  ( -0.000000000000000000, -0.3543493200069153248, -0.9351131265310291818 ) ) ;
#74302=LINE ( 'NONE', #19194, #79297 ) ;
#74303=ORIENTED_EDGE ( 'NONE', *, *, #116058, .T. ) ;
#74304=AXIS2_PLACEMENT_3D ( 'NONE', #52251, #61728, #31232 ) ;
#74305=CARTESIAN_POINT ( 'NONE',  ( 2.999999999999981792, 7.931123077392108200, 4.000000000000000000 ) ) ;
#74306=DIRECTION ( 'NONE',  ( 0.000000000000000000, -1.000000000000000000, 0.000000000000000000 ) ) ;
#74307=ORIENTED_EDGE ( 'NONE', *, *, #51078, .T. ) ;
#74310=VECTOR ( 'NONE', #40156, 999.9999999999998863 ) ;
#74311=EDGE_CURVE ( 'NONE', #60942, #106916, #5482, .T. ) ;
#74312=EDGE_LOOP ( 'NONE', ( #107622, #104412, #74345, #57426 ) ) ;
#74314=EDGE_LOOP ( 'NONE', ( #129161, #35617, #40913, #116487 ) ) ;
#74315=CARTESIAN_POINT ( 'NONE',  ( 28.17183060077627843, 9.759292476615620160, 4.000000000000000000 ) ) ;
#74316=VECTOR ( 'NONE', #97599, 1000.000000000000000 ) ;
#74320=ORIENTED_EDGE ( 'NONE', *, *, #111428, .F. ) ;
#74323=DIRECTION ( 'NONE',  ( 0.7071067811865487940, 0.7071067811865463515, 0.000000000000000000 ) ) ;
#74326=ADVANCED_FACE ( 'NONE', ( #27244 ), #72248, .F. ) ;
#74327=CARTESIAN_POINT ( 'NONE',  ( -1.499999999999990896, 18.43112307739199451, 4.000000000000000000 ) ) ;
#74328=ORIENTED_EDGE ( 'NONE', *, *, #110930, .F. ) ;
#74329=AXIS2_PLACEMENT_3D ( 'NONE', #16546, #135514, #58713 ) ;
#74331=CARTESIAN_POINT ( 'NONE',  ( -15.32816939922341781, -9.740707523384180888, 4.000000000000000000 ) ) ;
#74332=DIRECTION ( 'NONE',  ( 0.3543493200069162685, -0.000000000000000000, -0.9351131265310288487 ) ) ;
#74333=ORIENTED_EDGE ( 'NONE', *, *, #103177, .F. ) ;
#74334=FACE_OUTER_BOUND ( 'NONE', #83907, .T. ) ;
#74335=ORIENTED_EDGE ( 'NONE', *, *, #92943, .F. ) ;
#74336=ORIENTED_EDGE ( 'NONE', *, *, #92219, .F. ) ;
#74337=ORIENTED_EDGE ( 'NONE', *, *, #6979, .T. ) ;
#74338=DIRECTION ( 'NONE',  ( -0.7071067811865487940, 0.7071067811865463515, -0.000000000000000000 ) ) ;
#74339=ADVANCED_FACE ( 'NONE', ( #137463 ), #17105, .T. ) ;
#74340=VECTOR ( 'NONE', #35488, 1000.000000000000000 ) ;
#74342=DIRECTION ( 'NONE',  ( -0.000000000000000000, -0.3543493200069152693, 0.9351131265310292928 ) ) ;
#74343=CARTESIAN_POINT ( 'NONE',  ( -47.99451991528749062, 28.92564299267971251, 4.000000000000000000 ) ) ;
#74344=DIRECTION ( 'NONE',  ( -0.7071067811865486830, -0.7071067811865464625, 0.000000000000000000 ) ) ;
#74345=ORIENTED_EDGE ( 'NONE', *, *, #57796, .F. ) ;
#74346=DIRECTION ( 'NONE',  ( 0.7071067811865487940, 0.7071067811865463515, 0.000000000000000000 ) ) ;
#74347=ORIENTED_EDGE ( 'NONE', *, *, #72882, .F. ) ;
#74349=AXIS2_PLACEMENT_3D ( 'NONE', #34817, #23179, #67466 ) ;
#74351=EDGE_CURVE ( 'NONE', #96542, #94223, #47630, .T. ) ;
#74353=ORIENTED_EDGE ( 'NONE', *, *, #16527, .F. ) ;
#74354=FACE_OUTER_BOUND ( 'NONE', #121885, .T. ) ;
#74355=DIRECTION ( 'NONE',  ( -0.7071067811865487940, 0.7071067811865463515, 0.000000000000000000 ) ) ;
#74356=EDGE_LOOP ( 'NONE', ( #30356, #60248, #49529, #26841 ) ) ;
#74357=EDGE_LOOP ( 'NONE', ( #28084, #69403, #85755, #120227 ) ) ;
#74358=DIRECTION ( 'NONE',  ( 0.6830127018922181881, 0.6830127018922202975, -0.2588190451025214056 ) ) ;
#74359=DIRECTION ( 'NONE',  ( 0.000000000000000000, -0.3543493200069153248, 0.9351131265310292928 ) ) ;
#74360=CARTESIAN_POINT ( 'NONE',  ( 51.48921356237309510, -27.52281430457091460, 5.000000000000000000 ) ) ;
#74362=VECTOR ( 'NONE', #136357, 999.9999999999998863 ) ;
#74363=EDGE_CURVE ( 'NONE', #19902, #99485, #92496, .T. ) ;
#74366=CARTESIAN_POINT ( 'NONE',  ( -22.49999999999984368, 9.431123077392086884, 4.000000000000000000 ) ) ;
#74367=AXIS2_PLACEMENT_3D ( 'NONE', #11303, #12045, #132458 ) ;
#74368=AXIS2_PLACEMENT_3D ( 'NONE', #99176, #76035, #42715 ) ;
#74369=DIRECTION ( 'NONE',  ( 0.6830127018922180770, -0.6830127018922204085, -0.2588190451025213501 ) ) ;
#74370=DIRECTION ( 'NONE',  ( -0.7071067811865487940, 0.7071067811865463515, 0.000000000000000000 ) ) ;
#74372=ORIENTED_EDGE ( 'NONE', *, *, #117375, .T. ) ;
#74373=DIRECTION ( 'NONE',  ( -0.000000000000000000, 0.000000000000000000, 1.000000000000000000 ) ) ;
#74374=EDGE_LOOP ( 'NONE', ( #93304, #135951, #102759, #67393 ) ) ;
#74375=VECTOR ( 'NONE', #131215, 1000.000000000000114 ) ;
#74376=VECTOR ( 'NONE', #108927, 1000.000000000000000 ) ;
#74377=AXIS2_PLACEMENT_3D ( 'NONE', #32647, #66005, #87726 ) ;
#74378=DIRECTION ( 'NONE',  ( 0.6830127018922181881, 0.6830127018922202975, -0.2588190451025214056 ) ) ;
#74381=ORIENTED_EDGE ( 'NONE', *, *, #129377, .T. ) ;
#74382=VECTOR ( 'NONE', #34208, 1000.000000000000000 ) ;
#74383=FACE_OUTER_BOUND ( 'NONE', #104589, .T. ) ;
#74384=CARTESIAN_POINT ( 'NONE',  ( 29.16170612452601674, -6.740707523384216415, 16.75550250614874415 ) ) ;
#74385=ORIENTED_EDGE ( 'NONE', *, *, #98093, .T. ) ;
#74387=LINE ( 'NONE', #73657, #41747 ) ;
#74388=CARTESIAN_POINT ( 'NONE',  ( 23.99999999999983658, -4.447814304570781196, 5.000000000000000000 ) ) ;
#74389=ORIENTED_EDGE ( 'NONE', *, *, #42760, .F. ) ;
#74390=VERTEX_POINT ( 'NONE', #14939 ) ;
#74391=DIRECTION ( 'NONE',  ( 0.7071067811865486830, -0.7071067811865464625, -0.000000000000000000 ) ) ;
#74392=VECTOR ( 'NONE', #77979, 1000.000000000000000 ) ;
#74395=CARTESIAN_POINT ( 'NONE',  ( -32.67183060077624646, 8.259292476615637923, 4.000000000000000000 ) ) ;
#74396=CARTESIAN_POINT ( 'NONE',  ( 6.938893903907228378E-15, -16.44781430457067017, 5.000000000000000000 ) ) ;
#74397=ORIENTED_EDGE ( 'NONE', *, *, #1632, .F. ) ;
#74398=VECTOR ( 'NONE', #92071, 999.9999999999998863 ) ;
#74399=DIRECTION ( 'NONE',  ( -0.7071067811865487940, 0.7071067811865463515, 0.000000000000000000 ) ) ;
#74400=EDGE_CURVE ( 'NONE', #83675, #24719, #94640, .T. ) ;
#74401=DIRECTION ( 'NONE',  ( 0.7071067811865487940, 0.7071067811865463515, 0.000000000000000000 ) ) ;
#74403=ORIENTED_EDGE ( 'NONE', *, *, #130762, .F. ) ;
#74404=CIRCLE ( 'NONE', #120607, 3.378199999999997871 ) ;
#74406=ORIENTED_EDGE ( 'NONE', *, *, #12515, .F. ) ;
#74407=VECTOR ( 'NONE', #87609, 1000.000000000000000 ) ;
#74410=CARTESIAN_POINT ( 'NONE',  ( 30.65494483745363041, 5.259292476615662792, 12.77922209995901071 ) ) ;
#74411=LINE ( 'NONE', #140358, #111819 ) ;
#74414=CARTESIAN_POINT ( 'NONE',  ( 28.49999999999981171, 13.46639925780212366, 5.000000000000000000 ) ) ;
#74415=DIRECTION ( 'NONE',  ( -0.6830127018922180770, -0.6830127018922204085, -0.2588190451025213501 ) ) ;
#74416=DIRECTION ( 'NONE',  ( 0.7071067811865486830, -0.7071067811865464625, -0.000000000000000000 ) ) ;
#74418=AXIS2_PLACEMENT_3D ( 'NONE', #68862, #80446, #56585 ) ;
#74419=DIRECTION ( 'NONE',  ( -0.000000000000000000, 0.000000000000000000, 1.000000000000000000 ) ) ;
#74421=ORIENTED_EDGE ( 'NONE', *, *, #89514, .F. ) ;
#74422=EDGE_CURVE ( 'NONE', #23253, #28047, #51738, .T. ) ;
#74423=CARTESIAN_POINT ( 'NONE',  ( -8.207106781186491062, 18.75929247661553489, 5.000000000000000000 ) ) ;
#74425=ADVANCED_FACE ( 'NONE', ( #59907 ), #72955, .F. ) ;
#74431=EDGE_CURVE ( 'NONE', #91733, #130435, #114267, .T. ) ;
#74432=CARTESIAN_POINT ( 'NONE',  ( 28.49999999999981171, -4.533600742197688938, 5.000000000000000000 ) ) ;
#74433=LINE ( 'NONE', #20009, #92010 ) ;
#74435=DIRECTION ( 'NONE',  ( -0.7071067811865486830, -0.7071067811865464625, 0.000000000000000000 ) ) ;
#74436=DIRECTION ( 'NONE',  ( -0.7071067811865487940, 0.7071067811865463515, -0.000000000000000000 ) ) ;
#74437=VERTEX_POINT ( 'NONE', #26551 ) ;
#74439=CARTESIAN_POINT ( 'NONE',  ( -4.641757024588570424, 15.75929247661555088, 19.34181609438700633 ) ) ;
#74440=DIRECTION ( 'NONE',  ( 0.7071067811865487940, 0.7071067811865463515, 0.000000000000000000 ) ) ;
#74442=ORIENTED_EDGE ( 'NONE', *, *, #20735, .T. ) ;
#74443=DIRECTION ( 'NONE',  ( -0.000000000000000000, -0.3543493200069152693, 0.9351131265310292928 ) ) ;
#74444=VECTOR ( 'NONE', #131816, 1000.000000000000000 ) ;
#74445=CARTESIAN_POINT ( 'NONE',  ( 48.29974487139158867, -27.71228299555239971, 4.000000000000000000 ) ) ;
#74447=VECTOR ( 'NONE', #126547, 1000.000000000000227 ) ;
#74449=ORIENTED_EDGE ( 'NONE', *, *, #9161, .T. ) ;
#74450=ORIENTED_EDGE ( 'NONE', *, *, #60246, .F. ) ;
#74451=FACE_BOUND ( 'NONE', #76733, .T. ) ;
#74452=CARTESIAN_POINT ( 'NONE',  ( 22.49999999999984368, -17.56887692260762535, 4.000000000000000000 ) ) ;
#74453=CARTESIAN_POINT ( 'NONE',  ( 35.99451991528749772, 28.92564299267963079, 4.000000000000000000 ) ) ;
#74454=CARTESIAN_POINT ( 'NONE',  ( -41.99451991528749062, 28.92564299267967343, 4.000000000000000000 ) ) ;
#74456=VECTOR ( 'NONE', #85576, 1000.000000000000000 ) ;
#74457=LINE ( 'NONE', #54150, #34227 ) ;
#74458=FACE_OUTER_BOUND ( 'NONE', #63521, .T. ) ;
#74459=ORIENTED_EDGE ( 'NONE', *, *, #71021, .T. ) ;
#74460=VERTEX_POINT ( 'NONE', #140309 ) ;
#74461=ORIENTED_EDGE ( 'NONE', *, *, #104835, .T. ) ;
#74462=ORIENTED_EDGE ( 'NONE', *, *, #5989, .F. ) ;
#74464=VECTOR ( 'NONE', #91792, 1000.000000000000000 ) ;
#74465=DIRECTION ( 'NONE',  ( 0.000000000000000000, -0.3543493200069153803, -0.9351131265310292928 ) ) ;
#74466=EDGE_CURVE ( 'NONE', #101826, #43833, #141005, .T. ) ;
#74467=VECTOR ( 'NONE', #106720, 1000.000000000000000 ) ;
#74468=EDGE_CURVE ( 'NONE', #17205, #62844, #43155, .T. ) ;
#74470=AXIS2_PLACEMENT_3D ( 'NONE', #114190, #125067, #14157 ) ;
#74471=CARTESIAN_POINT ( 'NONE',  ( -48.48921356237309510, -27.52281430457089328, 5.000000000000000000 ) ) ;
#74472=VERTEX_POINT ( 'NONE', #63499 ) ;
#74473=CARTESIAN_POINT ( 'NONE',  ( 0.000000000000000000, 0.000000000000000000, 5.000000000000000000 ) ) ;
#74474=DIRECTION ( 'NONE',  ( 0.7071067811865487940, 0.7071067811865463515, 0.000000000000000000 ) ) ;
#74475=LINE ( 'NONE', #109218, #103690 ) ;
#74476=CARTESIAN_POINT ( 'NONE',  ( -33.29974487139158867, -27.71228299555229313, 4.000000000000000000 ) ) ;
#74477=VECTOR ( 'NONE', #93956, 1000.000000000000000 ) ;
#74480=DIRECTION ( 'NONE',  ( 0.6830127018922180770, -0.6830127018922204085, -0.2588190451025213501 ) ) ;
#74481=VERTEX_POINT ( 'NONE', #75085 ) ;
#74482=EDGE_CURVE ( 'NONE', #94079, #100675, #96757, .T. ) ;
#74484=CARTESIAN_POINT ( 'NONE',  ( 7.499999999999944045, 13.56627193232215767, -10.57019076586066930 ) ) ;
#74487=LINE ( 'NONE', #96184, #87520 ) ;
#74489=EDGE_CURVE ( 'NONE', #38622, #35249, #75782, .T. ) ;
#74490=PLANE ( 'NONE',  #96892 ) ;
#74491=EDGE_LOOP ( 'NONE', ( #96144, #10104, #19407, #17355 ) ) ;
#74493=ORIENTED_EDGE ( 'NONE', *, *, #135338, .F. ) ;
#74494=ORIENTED_EDGE ( 'NONE', *, *, #135044, .T. ) ;
#74496=DIRECTION ( 'NONE',  ( -0.6830127018922180770, -0.6830127018922204085, -0.2588190451025213501 ) ) ;
#74497=CARTESIAN_POINT ( 'NONE',  ( 0.000000000000000000, 0.000000000000000000, 5.000000000000000000 ) ) ;
#74499=CARTESIAN_POINT ( 'NONE',  ( 19.72673754300674176, 9.106605730562614909, 4.258036837949496167 ) ) ;
#74500=ADVANCED_FACE ( 'NONE', ( #130163 ), #87365, .T. ) ;
#74501=DIRECTION ( 'NONE',  ( -0.7071067811865486830, -0.7071067811865464625, 0.000000000000000000 ) ) ;
#74502=LINE ( 'NONE', #118688, #85731 ) ;
#74503=ADVANCED_FACE ( 'NONE', ( #6891 ), #118543, .F. ) ;
#74505=CARTESIAN_POINT ( 'NONE',  ( 0.000000000000000000, 0.000000000000000000, 5.000000000000000000 ) ) ;
#74507=DIRECTION ( 'NONE',  ( -0.000000000000000000, 0.000000000000000000, 1.000000000000000000 ) ) ;
#74509=VECTOR ( 'NONE', #96674, 1000.000000000000000 ) ;
#74512=VECTOR ( 'NONE', #97257, 1000.000000000000000 ) ;
#74515=ORIENTED_EDGE ( 'NONE', *, *, #19128, .T. ) ;
#74517=CARTESIAN_POINT ( 'NONE',  ( -54.18398860626899705, 28.73617430169825226, 5.000000000000000000 ) ) ;
#74518=DIRECTION ( 'NONE',  ( 0.7071067811865487940, 0.7071067811865463515, -0.000000000000000000 ) ) ;
#74519=LINE ( 'NONE', #118703, #74152 ) ;
#74520=ORIENTED_EDGE ( 'NONE', *, *, #107356, .F. ) ;
#74522=VERTEX_POINT ( 'NONE', #8326 ) ;
#74524=ADVANCED_FACE ( 'NONE', ( #130886 ), #20653, .T. ) ;
#74526=CARTESIAN_POINT ( 'NONE',  ( -33.18398860626899705, 28.73617430169810305, 5.000000000000000000 ) ) ;
#74527=DIRECTION ( 'NONE',  ( -0.7071067811865486830, -0.7071067811865464625, 0.000000000000000000 ) ) ;
#74529=ORIENTED_EDGE ( 'NONE', *, *, #89445, .F. ) ;
#74530=ORIENTED_EDGE ( 'NONE', *, *, #71029, .F. ) ;
#74531=AXIS2_PLACEMENT_3D ( 'NONE', #50696, #30363, #5729 ) ;
#74532=ORIENTED_EDGE ( 'NONE', *, *, #50517, .T. ) ;
#74533=CARTESIAN_POINT ( 'NONE',  ( -34.92500000000001137, -22.22500000000000142, 4.500000000000000888 ) ) ;
#74534=DIRECTION ( 'NONE',  ( -0.3543493200069163240, 0.000000000000000000, -0.9351131265310288487 ) ) ;
#74535=VECTOR ( 'NONE', #26921, 1000.000000000000000 ) ;
#74536=CARTESIAN_POINT ( 'NONE',  ( 24.29974487139158867, -27.71228299555223273, 4.000000000000000000 ) ) ;
#74537=FACE_OUTER_BOUND ( 'NONE', #80340, .T. ) ;
#74538=LINE ( 'NONE', #108526, #92001 ) ;
#74539=DIRECTION ( 'NONE',  ( -0.000000000000000000, -0.000000000000000000, 1.000000000000000000 ) ) ;
#74541=FACE_OUTER_BOUND ( 'NONE', #75044, .T. ) ;
#74543=ORIENTED_EDGE ( 'NONE', *, *, #9905, .F. ) ;
#74544=DIRECTION ( 'NONE',  ( 0.7071067811865487940, -0.7071067811865463515, 0.000000000000000000 ) ) ;
#74545=VECTOR ( 'NONE', #81491, 1000.000000000000000 ) ;
#74546=CARTESIAN_POINT ( 'NONE',  ( 6.328169399223481761, 14.25929247661557930, 4.000000000000000000 ) ) ;
#74547=VERTEX_POINT ( 'NONE', #19941 ) ;
#74548=CARTESIAN_POINT ( 'NONE',  ( 60.29974487139158867, -27.71228299555248142, 4.000000000000000000 ) ) ;
#74549=CARTESIAN_POINT ( 'NONE',  ( 0.000000000000000000, 0.000000000000000000, 5.000000000000000000 ) ) ;
#74550=VERTEX_POINT ( 'NONE', #32272 ) ;
#74551=DIRECTION ( 'NONE',  ( -0.7071067811865486830, -0.7071067811865464625, 0.000000000000000000 ) ) ;
#74553=ORIENTED_EDGE ( 'NONE', *, *, #6047, .F. ) ;
#74554=PLANE ( 'NONE',  #88346 ) ;
#74555=ORIENTED_EDGE ( 'NONE', *, *, #53652, .T. ) ;
#74559=LINE ( 'NONE', #87562, #127264 ) ;
#74560=LINE ( 'NONE', #7838, #111676 ) ;
#74561=CARTESIAN_POINT ( 'NONE',  ( 24.48921356237309510, -27.52281430457072631, 5.000000000000000000 ) ) ;
#74564=AXIS2_PLACEMENT_3D ( 'NONE', #58358, #93069, #72072 ) ;
#74565=AXIS2_PLACEMENT_3D ( 'NONE', #141535, #42240, #119739 ) ;
#74567=PLANE ( 'NONE',  #60564 ) ;
#74568=CARTESIAN_POINT ( 'NONE',  ( 19.05000000000000071, 3.174999999999997158, 4.000000000000000000 ) ) ;
#74569=ORIENTED_EDGE ( 'NONE', *, *, #29406, .T. ) ;
#74570=( BOUNDED_CURVE ( )  B_SPLINE_CURVE ( 3, ( #16993, #16232, #36586, #114839 ),
 .UNSPECIFIED., .F., .F. ) 
 B_SPLINE_CURVE_WITH_KNOTS ( ( 4, 4 ),
 ( 2.001653308786169649, 3.503810798801450854 ),
 .UNSPECIFIED. ) 
 CURVE ( )  GEOMETRIC_REPRESENTATION_ITEM ( )  RATIONAL_B_SPLINE_CURVE ( ( 1.000000000000000000, 0.8206354192515240564, 0.8206354192515240564, 1.000000000000000000 ) ) 
 REPRESENTATION_ITEM ( '' )  );
#74571=VERTEX_POINT ( 'NONE', #53285 ) ;
#74572=VECTOR ( 'NONE', #9543, 1000.000000000000000 ) ;
#74574=LINE ( 'NONE', #52779, #116156 ) ;
#74575=EDGE_LOOP ( 'NONE', ( #76807, #121892, #97712, #73207 ) ) ;
#74576=CARTESIAN_POINT ( 'NONE',  ( 63.18398860626900415, 28.73617430169831621, 5.000000000000000000 ) ) ;
#74577=CARTESIAN_POINT ( 'NONE',  ( -72.48921356237309510, -27.52281430457106026, 5.000000000000000000 ) ) ;
#74578=VECTOR ( 'NONE', #141806, 999.9999999999998863 ) ;
#74580=CARTESIAN_POINT ( 'NONE',  ( -19.49999999999987921, 16.18958161055400780, -11.56426086740815862 ) ) ;
#74581=VERTEX_POINT ( 'NONE', #64187 ) ;
#74582=CARTESIAN_POINT ( 'NONE',  ( -34.42500000000001137, 2.977185695429387824, 5.000000000000000000 ) ) ;
#74583=EDGE_CURVE ( 'NONE', #74923, #81473, #85198, .T. ) ;
#74584=CARTESIAN_POINT ( 'NONE',  ( 3.299744871391591339, -27.71228299555208352, 4.000000000000000000 ) ) ;
#74585=DIRECTION ( 'NONE',  ( 0.7071067811865486830, -0.7071067811865464625, -0.000000000000000000 ) ) ;
#74586=ADVANCED_FACE ( 'NONE', ( #64907 ), #76505, .T. ) ;
#74587=EDGE_CURVE ( 'NONE', #20582, #69099, #19244, .T. ) ;
#74588=LINE ( 'NONE', #31081, #81900 ) ;
#74589=DIRECTION ( 'NONE',  ( 1.000000000000000000, 0.000000000000000000, 0.000000000000000000 ) ) ;
#74591=CARTESIAN_POINT ( 'NONE',  ( -7.499999999999947597, 12.43112307739205669, 4.000000000000000000 ) ) ;
#74593=FACE_OUTER_BOUND ( 'NONE', #83952, .T. ) ;
#74594=FACE_OUTER_BOUND ( 'NONE', #17699, .T. ) ;
#74596=EDGE_CURVE ( 'NONE', #3936, #132792, #84522, .T. ) ;
#74597=VERTEX_POINT ( 'NONE', #7628 ) ;
#74600=ORIENTED_EDGE ( 'NONE', *, *, #83805, .F. ) ;
#74602=VERTEX_POINT ( 'NONE', #56206 ) ;
#74603=EDGE_CURVE ( 'NONE', #91909, #2221, #115347, .T. ) ;
#74605=CARTESIAN_POINT ( 'NONE',  ( -69.29974487139159578, -27.71228299555254537, 4.000000000000000000 ) ) ;
#74606=ORIENTED_EDGE ( 'NONE', *, *, #8861, .F. ) ;
#74607=CARTESIAN_POINT ( 'NONE',  ( 2.510786437626908008, -27.52281430457053446, 5.000000000000000000 ) ) ;
#74608=CARTESIAN_POINT ( 'NONE',  ( -30.29974487139158867, -27.71228299555227537, 4.000000000000000000 ) ) ;
#74609=EDGE_CURVE ( 'NONE', #57693, #142882, #101799, .T. ) ;
#74611=ORIENTED_EDGE ( 'NONE', *, *, #140993, .F. ) ;
#74617=DIRECTION ( 'NONE',  ( 0.6830127018922180770, -0.6830127018922204085, -0.2588190451025213501 ) ) ;
#74619=ORIENTED_EDGE ( 'NONE', *, *, #21008, .T. ) ;
#74620=EDGE_LOOP ( 'NONE', ( #108119, #116865, #115555, #44512 ) ) ;
#74621=DIRECTION ( 'NONE',  ( 0.3543493200069162685, -0.000000000000000000, -0.9351131265310288487 ) ) ;
#74622=CARTESIAN_POINT ( 'NONE',  ( -19.17183060077633172, -5.240707523384225297, 4.000000000000000000 ) ) ;
#74624=EDGE_CURVE ( 'NONE', #70462, #116635, #1033, .T. ) ;
#74626=LINE ( 'NONE', #5748, #13186 ) ;
#74627=CARTESIAN_POINT ( 'NONE',  ( 0.1561230773924129900, -22.22500000000000142, 4.000000000000000000 ) ) ;
#74628=ORIENTED_EDGE ( 'NONE', *, *, #88666, .T. ) ;
#74629=ORIENTED_EDGE ( 'NONE', *, *, #113395, .T. ) ;
#74630=CARTESIAN_POINT ( 'NONE',  ( 57.48921356237308800, -27.52281430457095368, 5.000000000000000000 ) ) ;
#74631=ORIENTED_EDGE ( 'NONE', *, *, #105336, .T. ) ;
#74632=VERTEX_POINT ( 'NONE', #11177 ) ;
#74633=VECTOR ( 'NONE', #10562, 999.9999999999998863 ) ;
#74634=EDGE_CURVE ( 'NONE', #36186, #66777, #35147, .T. ) ;
#74635=VECTOR ( 'NONE', #96255, 999.9999999999998863 ) ;
#74637=FACE_OUTER_BOUND ( 'NONE', #26655, .T. ) ;
#74638=LINE ( 'NONE', #89082, #75246 ) ;
#74639=VERTEX_POINT ( 'NONE', #314 ) ;
#74640=PLANE ( 'NONE',  #138533 ) ;
#74642=ADVANCED_FACE ( 'NONE', ( #22766 ), #67044, .F. ) ;
#74643=LINE ( 'NONE', #73215, #24765 ) ;
#74644=AXIS2_PLACEMENT_3D ( 'NONE', #121042, #2077, #132686 ) ;
#74645=CARTESIAN_POINT ( 'NONE',  ( -6.792893218813405909, -5.240707523384232402, 5.000000000000000000 ) ) ;
#74646=VECTOR ( 'NONE', #94894, 999.9999999999998863 ) ;
#74647=ORIENTED_EDGE ( 'NONE', *, *, #127599, .F. ) ;
#74648=EDGE_CURVE ( 'NONE', #109724, #90846, #65656, .T. ) ;
#74649=LINE ( 'NONE', #41270, #16255 ) ;
#74650=FACE_OUTER_BOUND ( 'NONE', #76303, .T. ) ;
#74651=ORIENTED_EDGE ( 'NONE', *, *, #87318, .F. ) ;
#74652=DIRECTION ( 'NONE',  ( 0.7071067811865486830, -0.7071067811865464625, -0.000000000000000000 ) ) ;
#74653=DIRECTION ( 'NONE',  ( 0.7071067811865487940, 0.7071067811865463515, 0.000000000000000000 ) ) ;
#74655=CARTESIAN_POINT ( 'NONE',  ( 41.99451991528749062, 28.92564299267967343, 4.000000000000000000 ) ) ;
#74656=ORIENTED_EDGE ( 'NONE', *, *, #101087, .F. ) ;
#74657=LINE ( 'NONE', #106512, #15747 ) ;
#74658=EDGE_LOOP ( 'NONE', ( #32460, #126920, #15766, #137206 ) ) ;
#74659=VERTEX_POINT ( 'NONE', #43864 ) ;
#74660=VECTOR ( 'NONE', #10877, 1000.000000000000000 ) ;
#74661=EDGE_CURVE ( 'NONE', #15122, #36919, #22082, .T. ) ;
#74662=ORIENTED_EDGE ( 'NONE', *, *, #101670, .T. ) ;
#74664=CARTESIAN_POINT ( 'NONE',  ( -2.816011393730999401, 28.73617430169785436, 5.000000000000000000 ) ) ;
#74665=LINE ( 'NONE', #118854, #139827 ) ;
#74668=ADVANCED_FACE ( 'NONE', ( #90205 ), #45320, .F. ) ;
#74669=CARTESIAN_POINT ( 'NONE',  ( 30.70710678118633652, 11.25929247661560773, 5.000000000000000000 ) ) ;
#74670=DIRECTION ( 'NONE',  ( -0.6830127018922181881, 0.6830127018922202975, -0.2588190451025214056 ) ) ;
#74671=VECTOR ( 'NONE', #115137, 1000.000000000000000 ) ;
#74673=VECTOR ( 'NONE', #142385, 999.9999999999998863 ) ;
#74674=DIRECTION ( 'NONE',  ( -0.3543493200069162685, -0.000000000000000000, -0.9351131265310288487 ) ) ;
#74675=AXIS2_PLACEMENT_3D ( 'NONE', #28688, #26529, #61344 ) ;
#74676=VECTOR ( 'NONE', #20949, 1000.000000000000000 ) ;
#74677=CARTESIAN_POINT ( 'NONE',  ( -48.18398860626899705, 28.73617430169820608, 5.000000000000000000 ) ) ;
#74678=DIRECTION ( 'NONE',  ( -0.7071067811865486830, 0.7071067811865464625, 0.000000000000000000 ) ) ;
#74679=CARTESIAN_POINT ( 'NONE',  ( -30.29974487139158867, -27.71228299555227537, 4.000000000000000000 ) ) ;
#74680=ORIENTED_EDGE ( 'NONE', *, *, #117997, .F. ) ;
#74681=EDGE_LOOP ( 'NONE', ( #84572, #17356, #110825, #95818 ) ) ;
#74682=VECTOR ( 'NONE', #113250, 1000.000000000000000 ) ;
#74684=VECTOR ( 'NONE', #9624, 1000.000000000000000 ) ;
#74685=EDGE_LOOP ( 'NONE', ( #109614, #106602, #135020, #87196 ) ) ;
#74686=STYLED_ITEM ( 'NONE', ( #65187 ), #34315 ) ;
#74688=ORIENTED_EDGE ( 'NONE', *, *, #41673, .F. ) ;
#74689=EDGE_LOOP ( 'NONE', ( #5119, #129761, #108919, #64645 ) ) ;
#74690=CARTESIAN_POINT ( 'NONE',  ( -13.49999999999990763, 6.431123077392117082, 4.000000000000000000 ) ) ;
#74691=DIRECTION ( 'NONE',  ( -0.3543493200069162685, -0.000000000000000000, -0.9351131265310288487 ) ) ;
#74693=DIRECTION ( 'NONE',  ( 0.3543493200069162685, -0.000000000000000000, -0.9351131265310288487 ) ) ;
#74695=ORIENTED_EDGE ( 'NONE', *, *, #615, .F. ) ;
#74696=CARTESIAN_POINT ( 'NONE',  ( -16.99806943317890173, -22.22500000000000142, 4.500000000000000888 ) ) ;
#74697=ORIENTED_EDGE ( 'NONE', *, *, #68569, .T. ) ;
#74698=CARTESIAN_POINT ( 'NONE',  ( -15.67180000000000284, 3.174999999999997158, 1.444000000000000394 ) ) ;
#74699=EDGE_CURVE ( 'NONE', #128485, #66817, #23520, .T. ) ;
#74700=CARTESIAN_POINT ( 'NONE',  ( 29.99451991528749417, 28.92564299267958816, 4.000000000000000000 ) ) ;
#74701=VECTOR ( 'NONE', #102543, 1000.000000000000227 ) ;
#74703=ORIENTED_EDGE ( 'NONE', *, *, #43420, .F. ) ;
#74705=DIRECTION ( 'NONE',  ( -0.7071067811865487940, 0.7071067811865463515, 0.000000000000000000 ) ) ;
#74706=CARTESIAN_POINT ( 'NONE',  ( 2.671830600776454734, 2.259292476615692546, 4.000000000000000000 ) ) ;
#74707=LINE ( 'NONE', #142103, #125257 ) ;
#74708=ORIENTED_EDGE ( 'NONE', *, *, #4492, .T. ) ;
#74709=ORIENTED_EDGE ( 'NONE', *, *, #102336, .T. ) ;
#74711=EDGE_LOOP ( 'NONE', ( #119647, #109835, #103638, #65248 ) ) ;
#74713=CARTESIAN_POINT ( 'NONE',  ( -9.489213562373095101, -27.52281430457062328, 5.000000000000000000 ) ) ;
#74714=DIRECTION ( 'NONE',  ( -0.7071067811865486830, -0.7071067811865464625, 0.000000000000000000 ) ) ;
#74715=CARTESIAN_POINT ( 'NONE',  ( 36.48921356237310221, -27.52281430457080802, 5.000000000000000000 ) ) ;
#74716=ORIENTED_EDGE ( 'NONE', *, *, #134996, .T. ) ;
#74717=EDGE_CURVE ( 'NONE', #108713, #89253, #68495, .T. ) ;
#74718=AXIS2_PLACEMENT_3D ( 'NONE', #97444, #86611, #19887 ) ;
#74720=EDGE_CURVE ( 'NONE', #126557, #72219, #77232, .T. ) ;
#74723=DIRECTION ( 'NONE',  ( -0.7071067811865487940, 0.7071067811865463515, -0.000000000000000000 ) ) ;
#74724=ORIENTED_EDGE ( 'NONE', *, *, #59320, .F. ) ;
#74725=PLANE ( 'NONE',  #92949 ) ;
#74726=FACE_OUTER_BOUND ( 'NONE', #68160, .T. ) ;
#74727=ORIENTED_EDGE ( 'NONE', *, *, #35355, .F. ) ;
#74730=ORIENTED_EDGE ( 'NONE', *, *, #128941, .T. ) ;
#74731=ADVANCED_FACE ( 'NONE', ( #138009 ), #50291, .F. ) ;
#74732=FACE_OUTER_BOUND ( 'NONE', #46074, .T. ) ;
#74733=DIRECTION ( 'NONE',  ( 0.6830127018922181881, 0.6830127018922202975, -0.2588190451025214056 ) ) ;
#74734=ORIENTED_EDGE ( 'NONE', *, *, #87596, .T. ) ;
#74736=CARTESIAN_POINT ( 'NONE',  ( -1.499999999999987566, 13.56627193232215056, -10.57019076586069062 ) ) ;
#74737=LINE ( 'NONE', #108016, #53036 ) ;
#74738=( BOUNDED_CURVE ( )  B_SPLINE_CURVE ( 3, ( #37950, #26348, #138692, #103868 ),
 .UNSPECIFIED., .F., .T. ) 
 B_SPLINE_CURVE_WITH_KNOTS ( ( 4, 4 ),
 ( 1.901594255663612065, 1.933014472006554740 ),
 .UNSPECIFIED. ) 
 CURVE ( )  GEOMETRIC_REPRESENTATION_ITEM ( )  RATIONAL_B_SPLINE_CURVE ( ( 1.000000000000000000, 0.9999177325257868620, 0.9999177325257868620, 1.000000000000000000 ) ) 
 REPRESENTATION_ITEM ( '' )  );
#74739=DIRECTION ( 'NONE',  ( 0.7071067811865487940, 0.7071067811865463515, -0.000000000000000000 ) ) ;
#74740=CARTESIAN_POINT ( 'NONE',  ( 34.92499999999998295, 16.70193056682081334, 4.500000000000000888 ) ) ;
#74742=AXIS2_PLACEMENT_3D ( 'NONE', #3775, #66946, #22677 ) ;
#74743=CARTESIAN_POINT ( 'NONE',  ( 10.49999999999993072, 9.431123077392090437, 4.000000000000000000 ) ) ;
#74744=PLANE ( 'NONE',  #14135 ) ;
#74745=DIRECTION ( 'NONE',  ( 0.7071067811865487940, -0.7071067811865463515, 0.000000000000000000 ) ) ;
#74746=DIRECTION ( 'NONE',  ( 0.7071067811865487940, 0.7071067811865463515, 0.000000000000000000 ) ) ;
#74747=AXIS2_PLACEMENT_3D ( 'NONE', #89534, #34444, #22121 ) ;
#74748=FACE_OUTER_BOUND ( 'NONE', #85428, .T. ) ;
#74751=ORIENTED_EDGE ( 'NONE', *, *, #108480, .T. ) ;
#74752=ORIENTED_EDGE ( 'NONE', *, *, #98817, .T. ) ;
#74753=EDGE_LOOP ( 'NONE', ( #132230, #95651, #15611, #84817 ) ) ;
#74756=EDGE_CURVE ( 'NONE', #55173, #53059, #61212, .T. ) ;
#74757=ORIENTED_EDGE ( 'NONE', *, *, #2742, .T. ) ;
#74759=DIRECTION ( 'NONE',  ( -0.7071067811865487940, 0.7071067811865463515, -0.000000000000000000 ) ) ;
#74760=DIRECTION ( 'NONE',  ( -0.3543493200069162685, -0.000000000000000000, -0.9351131265310288487 ) ) ;
#74761=VECTOR ( 'NONE', #13590, 1000.000000000000000 ) ;
#74762=VERTEX_POINT ( 'NONE', #92328 ) ;
#74763=DIRECTION ( 'NONE',  ( -0.000000000000000000, 0.3543493200069153248, 0.9351131265310292928 ) ) ;
#74764=EDGE_CURVE ( 'NONE', #84565, #140843, #91642, .T. ) ;
#74765=CARTESIAN_POINT ( 'NONE',  ( 10.82816939922345156, 18.75929247661552424, 4.000000000000000000 ) ) ;
#74766=CARTESIAN_POINT ( 'NONE',  ( -27.48921356237309155, -27.52281430457074762, 5.000000000000000000 ) ) ;
#74767=CARTESIAN_POINT ( 'NONE',  ( -72.48921356237309510, -27.52281430457106026, 5.000000000000000000 ) ) ;
#74769=ORIENTED_EDGE ( 'NONE', *, *, #86907, .T. ) ;
#74770=ADVANCED_FACE ( 'NONE', ( #94478 ), #103216, .F. ) ;
#74771=CARTESIAN_POINT ( 'NONE',  ( 22.56687199751243611, -21.74070752338406720, 6.915939825044020495 ) ) ;
#74772=CARTESIAN_POINT ( 'NONE',  ( -10.17183060077640278, 12.75929247661558996, 4.000000000000000000 ) ) ;
#74773=AXIS2_PLACEMENT_3D ( 'NONE', #73862, #16609, #93474 ) ;
#74774=DIRECTION ( 'NONE',  ( -0.7071067811865487940, 0.7071067811865463515, -0.000000000000000000 ) ) ;
#74775=DIRECTION ( 'NONE',  ( -0.3543493200069162685, -0.000000000000000000, -0.9351131265310288487 ) ) ;
#74778=EDGE_CURVE ( 'NONE', #31340, #95370, #4559, .T. ) ;
#74779=ADVANCED_FACE ( 'NONE', ( #125717 ), #27088, .F. ) ;
#74780=VERTEX_POINT ( 'NONE', #70645 ) ;
#74781=VERTEX_POINT ( 'NONE', #24937 ) ;
#74785=LINE ( 'NONE', #6590, #53277 ) ;
#74786=EDGE_CURVE ( 'NONE', #141528, #34917, #82922, .T. ) ;
#74787=CARTESIAN_POINT ( 'NONE',  ( 23.99999999999982947, 19.93112307739197675, 4.000000000000000000 ) ) ;
#74788=VECTOR ( 'NONE', #123400, 1000.000000000000227 ) ;
#74790=CARTESIAN_POINT ( 'NONE',  ( 23.54739889332687497, 7.099584588756134629, 5.000000000000000000 ) ) ;
#74791=CARTESIAN_POINT ( 'NONE',  ( 5.669897814527313784, 17.25929247661553845, 19.83885114516069947 ) ) ;
#74792=VECTOR ( 'NONE', #36520, 1000.000000000000000 ) ;
#74793=CARTESIAN_POINT ( 'NONE',  ( -27.70710678118634718, -9.740707523384177335, 5.000000000000000000 ) ) ;
#74795=VECTOR ( 'NONE', #132982, 1000.000000000000227 ) ;
#74796=EDGE_CURVE ( 'NONE', #122347, #52394, #104647, .T. ) ;
#74798=ORIENTED_EDGE ( 'NONE', *, *, #138809, .F. ) ;
#74800=ORIENTED_EDGE ( 'NONE', *, *, #46335, .T. ) ;
#74801=VECTOR ( 'NONE', #65611, 1000.000000000000000 ) ;
#74802=VECTOR ( 'NONE', #85981, 1000.000000000000000 ) ;
#74804=LINE ( 'NONE', #3595, #47833 ) ;
#74805=DIRECTION ( 'NONE',  ( 0.7071067811865486830, -0.7071067811865464625, -0.000000000000000000 ) ) ;
#74806=ADVANCED_FACE ( 'NONE', ( #27806 ), #5320, .F. ) ;
#74807=CARTESIAN_POINT ( 'NONE',  ( 17.16170612452609490, -6.740707523384205757, 16.75550250614871217 ) ) ;
#74808=ORIENTED_EDGE ( 'NONE', *, *, #58312, .T. ) ;
#74810=EDGE_LOOP ( 'NONE', ( #36592, #30631, #47293, #6170 ) ) ;
#74811=LINE ( 'NONE', #87790, #14426 ) ;
#74812=LINE ( 'NONE', #95809, #138781 ) ;
#74813=FACE_OUTER_BOUND ( 'NONE', #99150, .T. ) ;
#74814=CARTESIAN_POINT ( 'NONE',  ( -11.99451991528749417, 28.92564299267946382, 4.000000000000000000 ) ) ;
#74815=EDGE_CURVE ( 'NONE', #3936, #108682, #81509, .T. ) ;
#74817=VERTEX_POINT ( 'NONE', #36545 ) ;
#74818=CARTESIAN_POINT ( 'NONE',  ( 14.29298673570684919, -21.74070752338406365, 4.999753212805221558 ) ) ;
#74819=ORIENTED_EDGE ( 'NONE', *, *, #89348, .T. ) ;
#74820=ORIENTED_EDGE ( 'NONE', *, *, #70429, .T. ) ;
#74822=AXIS2_PLACEMENT_3D ( 'NONE', #129019, #29695, #118115 ) ;
#74826=ORIENTED_EDGE ( 'NONE', *, *, #119993, .F. ) ;
#74828=EDGE_CURVE ( 'NONE', #38388, #70673, #25660, .T. ) ;
#74829=CARTESIAN_POINT ( 'NONE',  ( 24.48921356237309510, -27.52281430457072631, 5.000000000000000000 ) ) ;
#74830=ADVANCED_FACE ( 'NONE', ( #114788 ), #113372, .F. ) ;
#74831=FACE_OUTER_BOUND ( 'NONE', #69250, .T. ) ;
#74832=FACE_BOUND ( 'NONE', #52950, .T. ) ;
#74833=EDGE_LOOP ( 'NONE', ( #27458, #33471, #31318, #78579 ) ) ;
#74834=LINE ( 'NONE', #8770, #119744 ) ;
#74835=DIRECTION ( 'NONE',  ( 0.7071067811865487940, -0.7071067811865463515, 0.000000000000000000 ) ) ;
#74836=CARTESIAN_POINT ( 'NONE',  ( 0.1839886062690032631, 28.73617430169787568, 5.000000000000000000 ) ) ;
#74837=VERTEX_POINT ( 'NONE', #116246 ) ;
#74838=CARTESIAN_POINT ( 'NONE',  ( -78.29974487139158157, -27.71228299555260577, 4.000000000000000000 ) ) ;
#74839=ORIENTED_EDGE ( 'NONE', *, *, #117089, .F. ) ;
#74840=ORIENTED_EDGE ( 'NONE', *, *, #6826, .T. ) ;
#74842=VERTEX_POINT ( 'NONE', #102540 ) ;
#74843=VECTOR ( 'NONE', #18885, 1000.000000000000000 ) ;
#74845=VECTOR ( 'NONE', #73624, 1000.000000000000000 ) ;
#74846=ORIENTED_EDGE ( 'NONE', *, *, #99080, .T. ) ;
#74847=PLANE ( 'NONE',  #32592 ) ;
#74848=CARTESIAN_POINT ( 'NONE',  ( 33.18398860626899705, 28.73617430169810305, 5.000000000000000000 ) ) ;
#74849=EDGE_CURVE ( 'NONE', #40992, #71472, #47474, .T. ) ;
#74850=VECTOR ( 'NONE', #107608, 1000.000000000000000 ) ;
#74852=CARTESIAN_POINT ( 'NONE',  ( 29.99999999999979039, 8.966399257802173395, 5.000000000000000000 ) ) ;
#74854=VECTOR ( 'NONE', #60149, 999.9999999999998863 ) ;
#74855=LINE ( 'NONE', #119032, #110331 ) ;
#74856=EDGE_CURVE ( 'NONE', #11235, #80300, #86488, .T. ) ;
#74857=LINE ( 'NONE', #29872, #85197 ) ;
#74858=CARTESIAN_POINT ( 'NONE',  ( -60.29974487139158867, -27.71228299555248142, 4.000000000000000000 ) ) ;
#74859=DIRECTION ( 'NONE',  ( -0.6830127018922180770, -0.6830127018922202975, -0.2588190451025213501 ) ) ;
#74860=CARTESIAN_POINT ( 'NONE',  ( 5.999999999999972466, 4.552185695429124657, 5.000000000000000000 ) ) ;
#74862=VECTOR ( 'NONE', #103069, 1000.000000000000000 ) ;
#74864=DIRECTION ( 'NONE',  ( 1.000000000000000000, 0.000000000000000000, 0.000000000000000000 ) ) ;
#74865=CARTESIAN_POINT ( 'NONE',  ( -27.18398860626900060, 28.73617430169806042, 5.000000000000000000 ) ) ;
#74866=ORIENTED_EDGE ( 'NONE', *, *, #134742, .F. ) ;
#74868=ORIENTED_EDGE ( 'NONE', *, *, #42171, .F. ) ;
#74869=DIRECTION ( 'NONE',  ( -0.7071067811865486830, 0.7071067811865464625, 0.000000000000000000 ) ) ;
#74870=CARTESIAN_POINT ( 'NONE',  ( 0.000000000000000000, -21.72500000000000142, 4.500000000000000888 ) ) ;
#74871=ADVANCED_FACE ( 'NONE', ( #42987 ), #95915, .F. ) ;
#74872=ADVANCED_FACE ( 'NONE', ( #9592 ), #108903, .F. ) ;
#74873=DIRECTION ( 'NONE',  ( 0.7071067811865486830, -0.7071067811865464625, -0.000000000000000000 ) ) ;
#74874=VECTOR ( 'NONE', #87965, 1000.000000000000000 ) ;
#74876=CARTESIAN_POINT ( 'NONE',  ( 18.18398860626898994, 28.73617430169800002, 5.000000000000000000 ) ) ;
#74877=LINE ( 'NONE', #107460, #7578 ) ;
#74879=ORIENTED_EDGE ( 'NONE', *, *, #53279, .T. ) ;
#74881=ADVANCED_FACE ( 'NONE', ( #116953 ), #127859, .T. ) ;
#74882=CARTESIAN_POINT ( 'NONE',  ( 0.000000000000000000, -19.06887692260762535, 4.000000000000000000 ) ) ;
#74883=DIRECTION ( 'NONE',  ( -0.7071067811865486830, 0.7071067811865464625, 0.000000000000000000 ) ) ;
#74886=ORIENTED_EDGE ( 'NONE', *, *, #100398, .T. ) ;
#74887=CARTESIAN_POINT ( 'NONE',  ( -22.49999999999984013, -20.94781430457062044, 5.000000000000000000 ) ) ;
#74888=VERTEX_POINT ( 'NONE', #74175 ) ;
#74889=CARTESIAN_POINT ( 'NONE',  ( -15.70710678118642711, -15.74070752338412404, 5.000000000000000000 ) ) ;
#74890=DIRECTION ( 'NONE',  ( 0.7071067811865487940, -0.7071067811865463515, 0.000000000000000000 ) ) ;
#74892=VECTOR ( 'NONE', #121170, 999.9999999999998863 ) ;
#74893=ORIENTED_EDGE ( 'NONE', *, *, #55397, .F. ) ;
#74895=CARTESIAN_POINT ( 'NONE',  ( -2.999999999999975131, -7.447814304570750998, 5.000000000000000000 ) ) ;
#74897=VECTOR ( 'NONE', #139684, 1000.000000000000000 ) ;
#74898=ORIENTED_EDGE ( 'NONE', *, *, #63013, .T. ) ;
#74899=FACE_OUTER_BOUND ( 'NONE', #104876, .T. ) ;
#74901=LINE ( 'NONE', #17608, #102506 ) ;
#74902=ORIENTED_EDGE ( 'NONE', *, *, #44684, .T. ) ;
#74904=DIRECTION ( 'NONE',  ( -0.7071067811865486830, 0.7071067811865464625, 0.000000000000000000 ) ) ;
#74905=EDGE_LOOP ( 'NONE', ( #9242, #40974, #9971, #5590 ) ) ;
#74906=EDGE_CURVE ( 'NONE', #130610, #84223, #30683, .T. ) ;
#74907=ORIENTED_EDGE ( 'NONE', *, *, #55659, .F. ) ;
#74908=CARTESIAN_POINT ( 'NONE',  ( 20.99451991528748707, 28.92564299267952777, 4.000000000000000000 ) ) ;
#74909=DIRECTION ( 'NONE',  ( -1.000000000000000000, 0.000000000000000000, 0.000000000000000000 ) ) ;
#74910=VECTOR ( 'NONE', #30613, 1000.000000000000000 ) ;
#74913=AXIS2_PLACEMENT_3D ( 'NONE', #87022, #111632, #44251 ) ;
#74914=DIRECTION ( 'NONE',  ( -0.000000000000000000, 0.3543493200069153248, 0.9351131265310292928 ) ) ;
#74915=DIRECTION ( 'NONE',  ( -0.000000000000000000, -0.3543493200069152693, 0.9351131265310292928 ) ) ;
#74916=EDGE_LOOP ( 'NONE', ( #3974, #32405, #125374, #93166 ) ) ;
#74918=DIRECTION ( 'NONE',  ( 0.3543493200069162685, -0.000000000000000000, -0.9351131265310288487 ) ) ;
#74919=DIRECTION ( 'NONE',  ( -0.000000000000000000, 0.3543493200069153248, 0.9351131265310292928 ) ) ;
#74920=LINE ( 'NONE', #53878, #1936 ) ;
#74922=CARTESIAN_POINT ( 'NONE',  ( -25.49999999999981526, 3.052185695429136647, 5.000000000000000000 ) ) ;
#74923=VERTEX_POINT ( 'NONE', #128555 ) ;
#74924=CARTESIAN_POINT ( 'NONE',  ( 2.999999999999976463, -19.22509904557636418, 1.855685503482186638 ) ) ;
#74925=AXIS2_PLACEMENT_3D ( 'NONE', #90175, #11890, #45292 ) ;
#74926=EDGE_LOOP ( 'NONE', ( #136463, #37899, #20190 ) ) ;
#74927=ORIENTED_EDGE ( 'NONE', *, *, #7460, .F. ) ;
#74928=DIRECTION ( 'NONE',  ( -0.000000000000000000, -0.3543493200069152693, 0.9351131265310292928 ) ) ;
#74929=CARTESIAN_POINT ( 'NONE',  ( -28.49999999999980460, 1.030536316426487797, -5.498701923753732679 ) ) ;
#74930=ORIENTED_EDGE ( 'NONE', *, *, #96129, .T. ) ;
#74931=DIRECTION ( 'NONE',  ( 0.3543493200069162685, -0.000000000000000000, -0.9351131265310288487 ) ) ;
#74932=LINE ( 'NONE', #19089, #113666 ) ;
#74933=VECTOR ( 'NONE', #119239, 1000.000000000000000 ) ;
#74934=FACE_OUTER_BOUND ( 'NONE', #28810, .T. ) ;
#74935=DIRECTION ( 'NONE',  ( -0.000000000000000000, 0.000000000000000000, 1.000000000000000000 ) ) ;
#74936=CARTESIAN_POINT ( 'NONE',  ( 24.29974487139158867, -27.71228299555223273, 4.000000000000000000 ) ) ;
#74937=ORIENTED_EDGE ( 'NONE', *, *, #74634, .T. ) ;
#74938=CARTESIAN_POINT ( 'NONE',  ( 32.87852683662832476, -20.24070752338407431, 7.412974875817714526 ) ) ;
#74939=DIRECTION ( 'NONE',  ( 0.6830127018922181881, 0.6830127018922202975, -0.2588190451025214056 ) ) ;
#74940=LINE ( 'NONE', #51749, #75120 ) ;
#74941=DIRECTION ( 'NONE',  ( -0.7071067811865487940, 0.7071067811865463515, 0.000000000000000000 ) ) ;
#74942=CARTESIAN_POINT ( 'NONE',  ( -5.206660635421487271, 21.75929247661549937, 4.998822639870708073 ) ) ;
#74944=CARTESIAN_POINT ( 'NONE',  ( 0.000000000000000000, 0.000000000000000000, 5.000000000000000000 ) ) ;
#74945=VECTOR ( 'NONE', #130278, 1000.000000000000114 ) ;
#74947=EDGE_CURVE ( 'NONE', #13986, #27362, #107504, .T. ) ;
#74949=CARTESIAN_POINT ( 'NONE',  ( -63.18398860626900415, 28.73617430169831621, 5.000000000000000000 ) ) ;
#74950=VERTEX_POINT ( 'NONE', #42276 ) ;
#74951=ORIENTED_EDGE ( 'NONE', *, *, #125148, .T. ) ;
#74953=LINE ( 'NONE', #116987, #128038 ) ;
#74954=EDGE_CURVE ( 'NONE', #113754, #16, #64721, .T. ) ;
#74955=CARTESIAN_POINT ( 'NONE',  ( 19.05000000000000071, 3.174999999999997158, 1.444000000000000394 ) ) ;
#74956=ADVANCED_FACE ( 'NONE', ( #140156 ), #6716, .F. ) ;
#74957=VECTOR ( 'NONE', #120920, 1000.000000000000000 ) ;
#74959=ORIENTED_EDGE ( 'NONE', *, *, #20755, .F. ) ;
#74960=EDGE_CURVE ( 'NONE', #68410, #86186, #72799, .T. ) ;
#74961=FACE_OUTER_BOUND ( 'NONE', #46705, .T. ) ;
#74963=EDGE_LOOP ( 'NONE', ( #54872, #104976, #32526, #24581 ) ) ;
#74964=CARTESIAN_POINT ( 'NONE',  ( 34.42499999999998295, -10.45860074219784330, 5.000000000000000000 ) ) ;
#74966=ORIENTED_EDGE ( 'NONE', *, *, #8281, .F. ) ;
#74967=DIRECTION ( 'NONE',  ( 0.7071067811865487940, -0.7071067811865463515, 0.000000000000000000 ) ) ;
#74968=CARTESIAN_POINT ( 'NONE',  ( -26.99999999999981526, -6.108550654416982972, -3.114665004255028791 ) ) ;
#74969=CARTESIAN_POINT ( 'NONE',  ( 34.42499999999998295, 0.000000000000000000, 4.500000000000000888 ) ) ;
#74970=EDGE_CURVE ( 'NONE', #121677, #60780, #63332, .T. ) ;
#74971=LINE ( 'NONE', #108967, #20868 ) ;
#74972=VERTEX_POINT ( 'NONE', #19068 ) ;
#74976=EDGE_LOOP ( 'NONE', ( #131143, #21040, #66801, #85663 ) ) ;
#74980=CIRCLE ( 'NONE', #130532, 5.968999999999998529 ) ;
#74983=ORIENTED_EDGE ( 'NONE', *, *, #11423, .F. ) ;
#74987=DIRECTION ( 'NONE',  ( -0.7071067811865486830, -0.7071067811865464625, 0.000000000000000000 ) ) ;
#74988=CARTESIAN_POINT ( 'NONE',  ( 30.29974487139158867, -27.71228299555227537, 4.000000000000000000 ) ) ;
#74989=DIRECTION ( 'NONE',  ( 0.6830127018922181881, 0.6830127018922202975, -0.2588190451025214056 ) ) ;
#74990=ORIENTED_EDGE ( 'NONE', *, *, #104853, .T. ) ;
#74991=ORIENTED_EDGE ( 'NONE', *, *, #54364, .F. ) ;
#74992=ADVANCED_FACE ( 'NONE', ( #18318 ), #62592, .F. ) ;
#74993=DIRECTION ( 'NONE',  ( -0.7071067811865487940, 0.7071067811865463515, 0.000000000000000000 ) ) ;
#74994=CARTESIAN_POINT ( 'NONE',  ( -8.999999999999928946, 4.552185695429119328, 5.000000000000000000 ) ) ;
#74995=VERTEX_POINT ( 'NONE', #51722 ) ;
#74996=AXIS2_PLACEMENT_3D ( 'NONE', #136132, #12206, #24518 ) ;
#74998=DIRECTION ( 'NONE',  ( 0.7071067811865487940, 0.7071067811865463515, -0.000000000000000000 ) ) ;
#75000=LINE ( 'NONE', #126647, #109413 ) ;
#75003=CARTESIAN_POINT ( 'NONE',  ( 66.29974487139159578, -27.71228299555252406, 4.000000000000000000 ) ) ;
#75004=FACE_BOUND ( 'NONE', #26881, .T. ) ;
#75005=DIRECTION ( 'NONE',  ( -0.6830127018922180770, -0.6830127018922204085, -0.2588190451025213501 ) ) ;
#75006=PLANE ( 'NONE',  #20230 ) ;
#75007=CARTESIAN_POINT ( 'NONE',  ( -31.49999999999977973, 8.900465351122127444, -2.516491619111439260 ) ) ;
#75008=ORIENTED_EDGE ( 'NONE', *, *, #8270, .T. ) ;
#75009=VECTOR ( 'NONE', #116369, 1000.000000000000000 ) ;
#75010=LINE ( 'NONE', #119184, #76502 ) ;
#75011=ADVANCED_FACE ( 'NONE', ( #56017 ), #1561, .F. ) ;
#75012=ORIENTED_EDGE ( 'NONE', *, *, #129800, .F. ) ;
#75013=VECTOR ( 'NONE', #102904, 999.9999999999998863 ) ;
#75014=ORIENTED_EDGE ( 'NONE', *, *, #19218, .F. ) ;
#75016=EDGE_LOOP ( 'NONE', ( #142061, #105180, #132602, #48029 ) ) ;
#75017=DIRECTION ( 'NONE',  ( -0.7071067811865486830, -0.7071067811865464625, -0.000000000000000000 ) ) ;
#75018=EDGE_CURVE ( 'NONE', #80227, #40577, #55284, .T. ) ;
#75019=ORIENTED_EDGE ( 'NONE', *, *, #135064, .T. ) ;
#75020=CARTESIAN_POINT ( 'NONE',  ( 30.79289321881324071, 12.75929247661559174, 5.000000000000000000 ) ) ;
#75021=VECTOR ( 'NONE', #79177, 999.9999999999998863 ) ;
#75022=DIRECTION ( 'NONE',  ( 0.6830127018922180770, -0.6830127018922204085, -0.2588190451025213501 ) ) ;
#75023=CARTESIAN_POINT ( 'NONE',  ( -3.489213562373097322, -27.52281430457057709, 5.000000000000000000 ) ) ;
#75024=DIRECTION ( 'NONE',  ( 0.7071067811865487940, 0.7071067811865463515, 0.000000000000000000 ) ) ;
#75025=VECTOR ( 'NONE', #77731, 1000.000000000000114 ) ;
#75026=EDGE_CURVE ( 'NONE', #56677, #129051, #22602, .T. ) ;
#75027=LINE ( 'NONE', #96022, #36662 ) ;
#75028=LINE ( 'NONE', #22029, #70535 ) ;
#75030=DIRECTION ( 'NONE',  ( -0.6830127018922181881, 0.6830127018922202975, -0.2588190451025214056 ) ) ;
#75031=VERTEX_POINT ( 'NONE', #12465 ) ;
#75033=EDGE_LOOP ( 'NONE', ( #109597, #15996, #124707 ) ) ;
#75034=LINE ( 'NONE', #73583, #91254 ) ;
#75035=( BOUNDED_CURVE ( )  B_SPLINE_CURVE ( 3, ( #114299, #61402, #49071, #72283 ),
 .UNSPECIFIED., .F., .T. ) 
 B_SPLINE_CURVE_WITH_KNOTS ( ( 4, 4 ),
 ( 5.043186909253412509, 5.074607125596327428 ),
 .UNSPECIFIED. ) 
 CURVE ( )  GEOMETRIC_REPRESENTATION_ITEM ( )  RATIONAL_B_SPLINE_CURVE ( ( 1.000000000000000000, 0.9999177325257868620, 0.9999177325257868620, 1.000000000000000000 ) ) 
 REPRESENTATION_ITEM ( '' )  );
#75036=DIRECTION ( 'NONE',  ( 0.6830127018922180770, -0.6830127018922204085, -0.2588190451025213501 ) ) ;
#75038=ORIENTED_EDGE ( 'NONE', *, *, #83284, .F. ) ;
#75039=ORIENTED_EDGE ( 'NONE', *, *, #73155, .F. ) ;
#75040=VECTOR ( 'NONE', #55985, 1000.000000000000000 ) ;
#75041=EDGE_CURVE ( 'NONE', #86087, #82492, #77752, .T. ) ;
#75044=EDGE_LOOP ( 'NONE', ( #104079, #30684, #49537, #101754 ) ) ;
#75046=VECTOR ( 'NONE', #67355, 1000.000000000000000 ) ;
#75047=AXIS2_PLACEMENT_3D ( 'NONE', #15435, #59724, #103884 ) ;
#75050=ORIENTED_EDGE ( 'NONE', *, *, #66766, .T. ) ;
#75051=LINE ( 'NONE', #106918, #142916 ) ;
#75052=VERTEX_POINT ( 'NONE', #65465 ) ;
#75053=CARTESIAN_POINT ( 'NONE',  ( 18.78162688292482230, 21.74787736706806740, 4.999607392498048419 ) ) ;
#75054=VECTOR ( 'NONE', #135161, 1000.000000000000000 ) ;
#75056=LINE ( 'NONE', #52549, #37875 ) ;
#75057=ORIENTED_EDGE ( 'NONE', *, *, #138826, .T. ) ;
#75059=DIRECTION ( 'NONE',  ( 0.7071067811865487940, -0.7071067811865463515, 0.000000000000000000 ) ) ;
#75060=DIRECTION ( 'NONE',  ( -0.000000000000000000, -0.000000000000000000, 1.000000000000000000 ) ) ;
#75061=EDGE_LOOP ( 'NONE', ( #22251, #116901, #68606, #82738 ) ) ;
#75064=VERTEX_POINT ( 'NONE', #67608 ) ;
#75065=EDGE_CURVE ( 'NONE', #43661, #40590, #32878, .T. ) ;
#75067=ORIENTED_EDGE ( 'NONE', *, *, #133808, .F. ) ;
#75068=DIRECTION ( 'NONE',  ( -0.7071067811865486830, -0.7071067811865464625, 0.000000000000000000 ) ) ;
#75069=VECTOR ( 'NONE', #29913, 1000.000000000000000 ) ;
#75072=LINE ( 'NONE', #93395, #125592 ) ;
#75073=CARTESIAN_POINT ( 'NONE',  ( -5.700255128608413102, -27.71228299555201957, 4.000000000000000000 ) ) ;
#75074=ADVANCED_FACE ( 'NONE', ( #132139 ), #54577, .F. ) ;
#75075=CARTESIAN_POINT ( 'NONE',  ( -56.99451991528749062, 28.92564299267978001, 4.000000000000000000 ) ) ;
#75076=ORIENTED_EDGE ( 'NONE', *, *, #20378, .T. ) ;
#75077=EDGE_CURVE ( 'NONE', #123227, #76657, #123414, .T. ) ;
#75078=CARTESIAN_POINT ( 'NONE',  ( 66.18398860626901126, 28.73617430169833753, 5.000000000000000000 ) ) ;
#75079=ORIENTED_EDGE ( 'NONE', *, *, #6295, .F. ) ;
#75080=CARTESIAN_POINT ( 'NONE',  ( -25.49999999999982236, 19.39370406404964697, 1.459788787078258876 ) ) ;
#75081=CARTESIAN_POINT ( 'NONE',  ( -12.70710678118645021, 2.259292476615694323, 5.000000000000000000 ) ) ;
#75082=VECTOR ( 'NONE', #139426, 1000.000000000000227 ) ;
#75083=VERTEX_POINT ( 'NONE', #100212 ) ;
#75084=DIRECTION ( 'NONE',  ( 0.6830127018922180770, -0.6830127018922204085, -0.2588190451025213501 ) ) ;
#75085=CARTESIAN_POINT ( 'NONE',  ( 22.17183060077631751, -8.240707523384200428, 4.000000000000000000 ) ) ;
#75086=VERTEX_POINT ( 'NONE', #32829 ) ;
#75087=ORIENTED_EDGE ( 'NONE', *, *, #137418, .T. ) ;
#75088=CARTESIAN_POINT ( 'NONE',  ( 39.18398860626899705, 28.73617430169814568, 5.000000000000000000 ) ) ;
#75089=CARTESIAN_POINT ( 'NONE',  ( -34.92500000000001137, -22.22500000000000142, 4.000000000000000000 ) ) ;
#75092=CARTESIAN_POINT ( 'NONE',  ( -34.92500000000001137, 7.067865804795134821, 10.74360474999298454 ) ) ;
#75095=EDGE_CURVE ( 'NONE', #93458, #82873, #15125, .T. ) ;
#75096=VECTOR ( 'NONE', #51652, 999.9999999999998863 ) ;
#75097=CARTESIAN_POINT ( 'NONE',  ( 27.18398860626900060, 28.73617430169806042, 5.000000000000000000 ) ) ;
#75098=CARTESIAN_POINT ( 'NONE',  ( -6.183988606268994381, 28.73617430169791476, 5.000000000000000000 ) ) ;
#75099=LINE ( 'NONE', #40329, #18874 ) ;
#75101=DIRECTION ( 'NONE',  ( -0.000000000000000000, 0.000000000000000000, 1.000000000000000000 ) ) ;
#75102=VERTEX_POINT ( 'NONE', #45849 ) ;
#75103=LINE ( 'NONE', #131600, #128766 ) ;
#75104=CARTESIAN_POINT ( 'NONE',  ( -36.18398860626899705, 28.73617430169812437, 5.000000000000000000 ) ) ;
#75105=VERTEX_POINT ( 'NONE', #66870 ) ;
#75106=CARTESIAN_POINT ( 'NONE',  ( 48.29974487139158867, -27.71228299555239971, 4.000000000000000000 ) ) ;
#75107=DIRECTION ( 'NONE',  ( 0.3543493200069163240, -0.000000000000000000, -0.9351131265310288487 ) ) ;
#75108=ORIENTED_EDGE ( 'NONE', *, *, #19912, .T. ) ;
#75109=PLANE ( 'NONE',  #85575 ) ;
#75110=CARTESIAN_POINT ( 'NONE',  ( 30.18398860626900060, 28.73617430169808173, 5.000000000000000000 ) ) ;
#75111=CARTESIAN_POINT ( 'NONE',  ( -33.48921356237309510, -27.52281430457078670, 5.000000000000000000 ) ) ;
#75112=ORIENTED_EDGE ( 'NONE', *, *, #22055, .T. ) ;
#75115=LINE ( 'NONE', #101829, #32891 ) ;
#75116=VECTOR ( 'NONE', #101560, 999.9999999999998863 ) ;
#75117=CARTESIAN_POINT ( 'NONE',  ( 81.29974487139159578, -27.71228299555262709, 4.000000000000000000 ) ) ;
#75119=FACE_OUTER_BOUND ( 'NONE', #106260, .T. ) ;
#75120=VECTOR ( 'NONE', #42308, 1000.000000000000000 ) ;
#75121=EDGE_CURVE ( 'NONE', #65792, #6819, #88630, .T. ) ;
#75122=LINE ( 'NONE', #96110, #71505 ) ;
#75123=VERTEX_POINT ( 'NONE', #11014 ) ;
#75124=CARTESIAN_POINT ( 'NONE',  ( -29.99451991528749417, 28.92564299267958816, 4.000000000000000000 ) ) ;
#75127=DIRECTION ( 'NONE',  ( -0.000000000000000000, 1.000000000000000000, -0.000000000000000000 ) ) ;
#75129=ORIENTED_EDGE ( 'NONE', *, *, #56575, .F. ) ;
#75130=EDGE_CURVE ( 'NONE', #34999, #106208, #43681, .T. ) ;
#75131=EDGE_CURVE ( 'NONE', #132715, #89674, #134268, .T. ) ;
#75132=DIRECTION ( 'NONE',  ( -0.000000000000000000, 0.000000000000000000, 1.000000000000000000 ) ) ;
#75133=ORIENTED_EDGE ( 'NONE', *, *, #111799, .F. ) ;
#75134=AXIS2_PLACEMENT_3D ( 'NONE', #5659, #36192, #48474 ) ;
#75135=AXIS2_PLACEMENT_3D ( 'NONE', #34289, #58238, #136442 ) ;
#75137=PLANE ( 'NONE',  #13045 ) ;
#75138=LINE ( 'NONE', #96813, #84107 ) ;
#75140=FACE_OUTER_BOUND ( 'NONE', #23468, .T. ) ;
#75141=DIRECTION ( 'NONE',  ( -0.7071067811865487940, 0.7071067811865463515, -0.000000000000000000 ) ) ;
#75142=ADVANCED_FACE ( 'NONE', ( #79209 ), #24075, .F. ) ;
#75144=CARTESIAN_POINT ( 'NONE',  ( 81.18398860626899705, 28.73617430169844056, 5.000000000000000000 ) ) ;
#75145=EDGE_CURVE ( 'NONE', #59489, #12358, #103566, .T. ) ;
#75146=DIRECTION ( 'NONE',  ( -0.6830127018922181881, 0.6830127018922202975, -0.2588190451025214056 ) ) ;
#75147=PLANE ( 'NONE',  #135439 ) ;
#75148=VERTEX_POINT ( 'NONE', #109646 ) ;
#75149=FACE_OUTER_BOUND ( 'NONE', #81195, .T. ) ;
#75150=LINE ( 'NONE', #40377, #140212 ) ;
#75151=CARTESIAN_POINT ( 'NONE',  ( 32.99451991528749062, 28.92564299267960948, 4.000000000000000000 ) ) ;
#75152=DIRECTION ( 'NONE',  ( 0.3543493200069162685, -0.000000000000000000, -0.9351131265310288487 ) ) ;
#75153=AXIS2_PLACEMENT_3D ( 'NONE', #25088, #91783, #25819 ) ;
#75154=EDGE_LOOP ( 'NONE', ( #2227, #115234, #31643, #72433 ) ) ;
#75155=EDGE_CURVE ( 'NONE', #79224, #56507, #10320, .T. ) ;
#75156=EDGE_LOOP ( 'NONE', ( #131509, #82728, #112129, #59404 ) ) ;
#75159=VECTOR ( 'NONE', #26020, 1000.000000000000000 ) ;
#75160=ORIENTED_EDGE ( 'NONE', *, *, #15049, .F. ) ;
#75161=CARTESIAN_POINT ( 'NONE',  ( 17.70025512860841488, -27.71228299555193786, 4.000000000000000000 ) ) ;
#75162=DIRECTION ( 'NONE',  ( 0.7071067811865487940, -0.7071067811865463515, 0.000000000000000000 ) ) ;
#75163=LINE ( 'NONE', #51250, #80516 ) ;
#75164=DIRECTION ( 'NONE',  ( -0.7071067811865487940, 0.7071067811865463515, 0.000000000000000000 ) ) ;
#75165=ORIENTED_EDGE ( 'NONE', *, *, #76462, .F. ) ;
#75166=EDGE_CURVE ( 'NONE', #31876, #138628, #127481, .T. ) ;
#75167=CARTESIAN_POINT ( 'NONE',  ( -3.812461875839445291, -22.22500000000000142, 4.000000000000000000 ) ) ;
#75169=AXIS2_PLACEMENT_3D ( 'NONE', #5429, #72910, #95313 ) ;
#75170=ORIENTED_EDGE ( 'NONE', *, *, #87824, .F. ) ;
#75171=PLANE ( 'NONE',  #368 ) ;
#75172=FACE_OUTER_BOUND ( 'NONE', #95712, .T. ) ;
#75173=EDGE_CURVE ( 'NONE', #125882, #2713, #95560, .T. ) ;
#75174=DIRECTION ( 'NONE',  ( -0.6830127018922180770, -0.6830127018922204085, -0.2588190451025213501 ) ) ;
#75175=VERTEX_POINT ( 'NONE', #84695 ) ;
#75176=ORIENTED_EDGE ( 'NONE', *, *, #52482, .F. ) ;
#75177=DIRECTION ( 'NONE',  ( -0.7071067811865486830, -0.7071067811865464625, 0.000000000000000000 ) ) ;
#75179=EDGE_CURVE ( 'NONE', #79735, #71611, #7086, .T. ) ;
#75180=PLANE ( 'NONE',  #51283 ) ;
#75181=LINE ( 'NONE', #132428, #48285 ) ;
#75182=EDGE_CURVE ( 'NONE', #126053, #132490, #50636, .T. ) ;
#75184=CARTESIAN_POINT ( 'NONE',  ( -26.99999999999981881, -19.06887692260762179, 4.000000000000000000 ) ) ;
#75187=EDGE_LOOP ( 'NONE', ( #130135, #136125, #31394, #12816 ) ) ;
#75190=ORIENTED_EDGE ( 'NONE', *, *, #62000, .F. ) ;
#75191=CARTESIAN_POINT ( 'NONE',  ( -15.70701326429294475, -21.74070752338406365, 4.999753212805219782 ) ) ;
#75192=AXIS2_PLACEMENT_3D ( 'NONE', #84807, #117404, #128330 ) ;
#75193=DIRECTION ( 'NONE',  ( -0.6830127018922180770, -0.6830127018922204085, -0.2588190451025213501 ) ) ;
#75194=CARTESIAN_POINT ( 'NONE',  ( 2.207106781186532363, 0.7592924766157069794, 5.000000000000000000 ) ) ;
#75195=ORIENTED_EDGE ( 'NONE', *, *, #72476, .F. ) ;
#75197=PLANE ( 'NONE',  #77277 ) ;
#75198=DIRECTION ( 'NONE',  ( 0.7071067811865487940, 0.7071067811865463515, 0.000000000000000000 ) ) ;
#75199=CARTESIAN_POINT ( 'NONE',  ( -13.82816939922342669, 21.75929247661550647, 4.000000000000000000 ) ) ;
#75200=LINE ( 'NONE', #130287, #113908 ) ;
#75202=DIRECTION ( 'NONE',  ( -0.000000000000000000, 0.3543493200069153248, 0.9351131265310292928 ) ) ;
#75203=CARTESIAN_POINT ( 'NONE',  ( 13.17183060077637613, -14.24070752338414181, 4.000000000000000000 ) ) ;
#75204=ORIENTED_EDGE ( 'NONE', *, *, #141170, .F. ) ;
#75206=ORIENTED_EDGE ( 'NONE', *, *, #60003, .F. ) ;
#75207=ORIENTED_EDGE ( 'NONE', *, *, #7603, .T. ) ;
#75208=ORIENTED_EDGE ( 'NONE', *, *, #107117, .T. ) ;
#75210=EDGE_LOOP ( 'NONE', ( #22874, #45392, #76014, #44979 ) ) ;
#75212=LINE ( 'NONE', #55592, #120736 ) ;
#75216=CARTESIAN_POINT ( 'NONE',  ( -18.75860074219783868, 21.72500000000000853, 5.000000000000000000 ) ) ;
#75217=AXIS2_PLACEMENT_3D ( 'NONE', #100241, #10350, #1595 ) ;
#75218=EDGE_CURVE ( 'NONE', #128354, #19651, #72438, .T. ) ;
#75220=ORIENTED_EDGE ( 'NONE', *, *, #99995, .T. ) ;
#75221=DIRECTION ( 'NONE',  ( 0.3543493200069162685, -0.000000000000000000, -0.9351131265310288487 ) ) ;
#75222=DIRECTION ( 'NONE',  ( -0.7071067811865486830, -0.7071067811865464625, 0.000000000000000000 ) ) ;
#75224=LINE ( 'NONE', #41134, #119188 ) ;
#75225=ORIENTED_EDGE ( 'NONE', *, *, #61456, .F. ) ;
#75226=DIRECTION ( 'NONE',  ( -0.000000000000000000, 0.000000000000000000, 1.000000000000000000 ) ) ;
#75227=ORIENTED_EDGE ( 'NONE', *, *, #74135, .T. ) ;
#75228=ORIENTED_EDGE ( 'NONE', *, *, #141966, .T. ) ;
#75229=ORIENTED_EDGE ( 'NONE', *, *, #65527, .T. ) ;
#75231=VERTEX_POINT ( 'NONE', #117991 ) ;
#75232=PLANE ( 'NONE',  #104802 ) ;
#75233=DIRECTION ( 'NONE',  ( -0.3543493200069162685, -0.000000000000000000, -0.9351131265310288487 ) ) ;
#75234=EDGE_CURVE ( 'NONE', #27746, #107457, #128898, .T. ) ;
#75235=CARTESIAN_POINT ( 'NONE',  ( 34.75611968250419181, 13.70565069852390927, 4.955485411084884717 ) ) ;
#75236=ORIENTED_EDGE ( 'NONE', *, *, #52520, .F. ) ;
#75239=ORIENTED_EDGE ( 'NONE', *, *, #137980, .F. ) ;
#75240=VECTOR ( 'NONE', #31600, 1000.000000000000000 ) ;
#75243=DIRECTION ( 'NONE',  ( 0.6830127018922180770, -0.6830127018922204085, -0.2588190451025213501 ) ) ;
#75244=VECTOR ( 'NONE', #89637, 1000.000000000000000 ) ;
#75245=CARTESIAN_POINT ( 'NONE',  ( 48.18398860626899705, 28.73617430169820608, 5.000000000000000000 ) ) ;
#75246=VECTOR ( 'NONE', #143432, 1000.000000000000227 ) ;
#75247=EDGE_CURVE ( 'NONE', #81137, #11235, #17286, .T. ) ;
#75248=CARTESIAN_POINT ( 'NONE',  ( -72.18398860626899705, 28.73617430169837661, 5.000000000000000000 ) ) ;
#75249=VERTEX_POINT ( 'NONE', #61550 ) ;
#75250=ORIENTED_EDGE ( 'NONE', *, *, #61206, .F. ) ;
#75251=ORIENTED_EDGE ( 'NONE', *, *, #43023, .T. ) ;
#75252=CARTESIAN_POINT ( 'NONE',  ( 13.17183060077637613, 21.75929247661549937, 4.000000000000000000 ) ) ;
#75255=DIRECTION ( 'NONE',  ( -0.7071067811865486830, -0.7071067811865464625, 0.000000000000000000 ) ) ;
#75256=ADVANCED_FACE ( 'NONE', ( #18694 ), #62970, .T. ) ;
#75257=FACE_OUTER_BOUND ( 'NONE', #56624, .T. ) ;
#75259=CARTESIAN_POINT ( 'NONE',  ( 11.99451991528749417, 28.92564299267946382, 4.000000000000000000 ) ) ;
#75261=ORIENTED_EDGE ( 'NONE', *, *, #39775, .T. ) ;
#75262=PLANE ( 'NONE',  #55772 ) ;
#75263=ORIENTED_EDGE ( 'NONE', *, *, #115532, .T. ) ;
#75264=EDGE_CURVE ( 'NONE', #12119, #122337, #26739, .T. ) ;
#75265=DIRECTION ( 'NONE',  ( -0.6830127018922180770, -0.6830127018922204085, -0.2588190451025213501 ) ) ;
#75266=VERTEX_POINT ( 'NONE', #94823 ) ;
#75268=VERTEX_POINT ( 'NONE', #37642 ) ;
#75269=LINE ( 'NONE', #41177, #39909 ) ;
#75270=EDGE_LOOP ( 'NONE', ( #23673, #4633, #20201, #36110, #67092, #21072, #136314, #91925, #45042, #79648, #112836, #98581, #120853, #115283, #94641, #69470, #40795, #2913, #69649, #99106, #81352, #56885, #63413, #143467, #74751, #22236, #117072, #62077, #107325, #53427, #77565, #66373, #105307, #63287, #58188, #30754, #61226, #40144, #62875, #40288, #24524, #100857, #127670, #86331 ) ) ;
#75271=EDGE_LOOP ( 'NONE', ( #113247, #116387, #34988, #7314 ) ) ;
#75272=DIRECTION ( 'NONE',  ( -0.7071067811865487940, 0.7071067811865463515, -0.000000000000000000 ) ) ;
#75273=ORIENTED_EDGE ( 'NONE', *, *, #11354, .F. ) ;
#75274=DIRECTION ( 'NONE',  ( 0.7071067811865487940, 0.7071067811865463515, 0.000000000000000000 ) ) ;
#75277=CARTESIAN_POINT ( 'NONE',  ( -14.70025512860841133, -27.71228299555195917, 4.000000000000000000 ) ) ;
#75278=DIRECTION ( 'NONE',  ( 0.7071067811865487940, 0.7071067811865463515, 0.000000000000000000 ) ) ;
#75279=LINE ( 'NONE', #45521, #128288 ) ;
#75280=ADVANCED_FACE ( 'NONE', ( #139087 ), #39792, .F. ) ;
#75281=DIRECTION ( 'NONE',  ( -0.7071067811865486830, 0.7071067811865464625, 0.000000000000000000 ) ) ;
#75284=LINE ( 'NONE', #45525, #16518 ) ;
#75286=ORIENTED_EDGE ( 'NONE', *, *, #81999, .F. ) ;
#75287=EDGE_CURVE ( 'NONE', #85316, #29037, #128214, .T. ) ;
#75288=ORIENTED_EDGE ( 'NONE', *, *, #7093, .T. ) ;
#75289=EDGE_CURVE ( 'NONE', #112409, #626, #60105, .T. ) ;
#75291=EDGE_LOOP ( 'NONE', ( #100663, #107940, #65604, #31769 ) ) ;
#75292=CARTESIAN_POINT ( 'NONE',  ( -16.49999999999988631, 10.46639925780215918, 5.000000000000000000 ) ) ;
#75293=CARTESIAN_POINT ( 'NONE',  ( 33.32816939922329880, -15.74070752338412760, 4.000000000000000000 ) ) ;
#75295=VERTEX_POINT ( 'NONE', #28892 ) ;
#75296=EDGE_CURVE ( 'NONE', #20428, #84993, #15812, .T. ) ;
#75297=LINE ( 'NONE', #80301, #85890 ) ;
#75298=DIRECTION ( 'NONE',  ( -0.6830127018922180770, -0.6830127018922204085, -0.2588190451025213501 ) ) ;
#75299=EDGE_CURVE ( 'NONE', #122251, #138807, #82556, .T. ) ;
#75301=DIRECTION ( 'NONE',  ( 0.7071067811865486830, -0.7071067811865464625, -0.000000000000000000 ) ) ;
#75303=ORIENTED_EDGE ( 'NONE', *, *, #57855, .F. ) ;
#75304=CARTESIAN_POINT ( 'NONE',  ( -10.49999999999993250, 10.94296225409025958, -9.576120664313281239 ) ) ;
#75308=ORIENTED_EDGE ( 'NONE', *, *, #28880, .T. ) ;
#75309=AXIS2_PLACEMENT_3D ( 'NONE', #51237, #18552, #85256 ) ;
#75311=VERTEX_POINT ( 'NONE', #43339 ) ;
#75314=EDGE_CURVE ( 'NONE', #57383, #55894, #20125, .T. ) ;
#75315=VECTOR ( 'NONE', #49463, 1000.000000000000000 ) ;
#75316=DIRECTION ( 'NONE',  ( -0.7071067811865486830, 0.7071067811865464625, 0.000000000000000000 ) ) ;
#75318=EDGE_LOOP ( 'NONE', ( #80185, #103190, #141826, #120624 ) ) ;
#75319=ADVANCED_FACE ( 'NONE', ( #20848 ), #9219, .F. ) ;
#75320=LINE ( 'NONE', #1968, #56023 ) ;
#75321=CARTESIAN_POINT ( 'NONE',  ( 2.700255128608413990, -27.71228299555204089, 4.000000000000000000 ) ) ;
#75323=VECTOR ( 'NONE', #104467, 999.9999999999998863 ) ;
#75324=ORIENTED_EDGE ( 'NONE', *, *, #27952, .T. ) ;
#75325=LINE ( 'NONE', #22314, #141556 ) ;
#75329=VERTEX_POINT ( 'NONE', #76704 ) ;
#75330=ORIENTED_EDGE ( 'NONE', *, *, #11583, .T. ) ;
#75331=ORIENTED_EDGE ( 'NONE', *, *, #67032, .T. ) ;
#75332=PLANE ( 'NONE',  #23629 ) ;
#75333=LINE ( 'NONE', #131128, #112549 ) ;
#75336=AXIS2_PLACEMENT_3D ( 'NONE', #60891, #15170, #59450 ) ;
#75337=PLANE ( 'NONE',  #30190 ) ;
#75338=EDGE_CURVE ( 'NONE', #42695, #81804, #31743, .T. ) ;
#75339=AXIS2_PLACEMENT_3D ( 'NONE', #54015, #19212, #131548 ) ;
#75340=EDGE_CURVE ( 'NONE', #2943, #20392, #121588, .T. ) ;
#75342=EDGE_LOOP ( 'NONE', ( #14962, #9586, #122026, #36283 ) ) ;
#75343=VECTOR ( 'NONE', #2925, 1000.000000000000114 ) ;
#75344=EDGE_LOOP ( 'NONE', ( #53458, #18272, #136180 ) ) ;
#75345=CARTESIAN_POINT ( 'NONE',  ( -21.96495920677946856, -2.033836129387410985, 4.000000000000000000 ) ) ;
#75346=ORIENTED_EDGE ( 'NONE', *, *, #102732, .F. ) ;
#75347=ORIENTED_EDGE ( 'NONE', *, *, #13932, .F. ) ;
#75353=LINE ( 'NONE', #29668, #110856 ) ;
#75354=CARTESIAN_POINT ( 'NONE',  ( -26.99999999999981171, 10.55218569542906160, 5.000000000000000000 ) ) ;
#75355=VERTEX_POINT ( 'NONE', #132524 ) ;
#75356=CARTESIAN_POINT ( 'NONE',  ( -42.29974487139158157, -27.71228299555235708, 4.000000000000000000 ) ) ;
#75357=ORIENTED_EDGE ( 'NONE', *, *, #106648, .F. ) ;
#75358=CARTESIAN_POINT ( 'NONE',  ( 24.48921356237309510, -27.52281430457072631, 5.000000000000000000 ) ) ;
#75359=CARTESIAN_POINT ( 'NONE',  ( 20.99451991528748707, 28.92564299267952777, 4.000000000000000000 ) ) ;
#75360=ORIENTED_EDGE ( 'NONE', *, *, #79535, .T. ) ;
#75361=LINE ( 'NONE', #20223, #74676 ) ;
#75362=EDGE_LOOP ( 'NONE', ( #99254, #124471, #51505, #58009 ) ) ;
#75364=VERTEX_POINT ( 'NONE', #87551 ) ;
#75366=EDGE_LOOP ( 'NONE', ( #63516, #51573, #47465, #87933 ) ) ;
#75368=CARTESIAN_POINT ( 'NONE',  ( -34.42500000000001137, -22.22500000000000142, 5.000000000000000000 ) ) ;
#75369=CARTESIAN_POINT ( 'NONE',  ( -1.567156510475481435, -22.22500000000000142, -7.640533879852384302 ) ) ;
#75371=EDGE_CURVE ( 'NONE', #89781, #13143, #53499, .T. ) ;
#75372=PLANE ( 'NONE',  #122306 ) ;
#75373=PLANE ( 'NONE',  #25031 ) ;
#75374=FACE_OUTER_BOUND ( 'NONE', #28890, .T. ) ;
#75375=DIRECTION ( 'NONE',  ( -0.7071067811865486830, -0.7071067811865464625, 0.000000000000000000 ) ) ;
#75376=FACE_OUTER_BOUND ( 'NONE', #55365, .T. ) ;
#75377=CARTESIAN_POINT ( 'NONE',  ( 36.48921356237310221, -27.52281430457080802, 5.000000000000000000 ) ) ;
#75378=ORIENTED_EDGE ( 'NONE', *, *, #68796, .F. ) ;
#75379=ORIENTED_EDGE ( 'NONE', *, *, #129106, .T. ) ;
#75380=ORIENTED_EDGE ( 'NONE', *, *, #22020, .T. ) ;
#75382=DIRECTION ( 'NONE',  ( -0.6830127018922180770, -0.6830127018922204085, -0.2588190451025213501 ) ) ;
#75383=ORIENTED_EDGE ( 'NONE', *, *, #17298, .F. ) ;
#75384=EDGE_CURVE ( 'NONE', #38574, #87786, #141958, .T. ) ;
#75385=ORIENTED_EDGE ( 'NONE', *, *, #8095, .T. ) ;
#75386=PLANE ( 'NONE',  #65314 ) ;
#75387=EDGE_CURVE ( 'NONE', #91904, #117764, #22257, .T. ) ;
#75388=EDGE_CURVE ( 'NONE', #116419, #59816, #10666, .T. ) ;
#75389=CARTESIAN_POINT ( 'NONE',  ( 14.99451991528749595, 28.92564299267948513, 4.000000000000000000 ) ) ;
#75390=EDGE_LOOP ( 'NONE', ( #111863, #54985, #23474, #33795 ) ) ;
#75391=CARTESIAN_POINT ( 'NONE',  ( 23.99999999999983302, -0.1606350220012988939, 4.664761815935144718 ) ) ;
#75392=EDGE_LOOP ( 'NONE', ( #70296, #47682, #104077, #128493 ) ) ;
#75393=DIRECTION ( 'NONE',  ( -0.3543493200069162685, -0.000000000000000000, -0.9351131265310288487 ) ) ;
#75394=EDGE_CURVE ( 'NONE', #116862, #111356, #109296, .T. ) ;
#75397=LINE ( 'NONE', #51511, #95910 ) ;
#75399=ORIENTED_EDGE ( 'NONE', *, *, #17957, .T. ) ;
#75403=EDGE_CURVE ( 'NONE', #27017, #89318, #75269, .T. ) ;
#75404=CARTESIAN_POINT ( 'NONE',  ( -32.29289321881323360, -6.740707523384211086, 5.000000000000000000 ) ) ;
#75405=CARTESIAN_POINT ( 'NONE',  ( -0.1839886062690032631, 28.73617430169787568, 5.000000000000000000 ) ) ;
#75406=ORIENTED_EDGE ( 'NONE', *, *, #133863, .F. ) ;
#75409=EDGE_LOOP ( 'NONE', ( #140651, #28971, #13797, #1843, #51049, #74328 ) ) ;
#75410=FACE_OUTER_BOUND ( 'NONE', #13225, .T. ) ;
#75411=CARTESIAN_POINT ( 'NONE',  ( 18.48921356237309510, -27.52281430457068367, 5.000000000000000000 ) ) ;
#75412=FACE_OUTER_BOUND ( 'NONE', #79872, .T. ) ;
#75413=CARTESIAN_POINT ( 'NONE',  ( -10.43312800248735606, -21.74070752338405654, 6.915939825044099543 ) ) ;
#75414=( BOUNDED_CURVE ( )  B_SPLINE_CURVE ( 3, ( #139241, #138507, #28327, #50782 ),
 .UNSPECIFIED., .F., .F. ) 
 B_SPLINE_CURVE_WITH_KNOTS ( ( 4, 4 ),
 ( 5.920967161967927161, 7.341195215986580536 ),
 .UNSPECIFIED. ) 
 CURVE ( )  GEOMETRIC_REPRESENTATION_ITEM ( )  RATIONAL_B_SPLINE_CURVE ( ( 1.000000000000000000, 0.8388583629366737071, 0.8388583629366737071, 1.000000000000000000 ) ) 
 REPRESENTATION_ITEM ( '' )  );
#75415=ORIENTED_EDGE ( 'NONE', *, *, #27284, .F. ) ;
#75416=CARTESIAN_POINT ( 'NONE',  ( 0.000000000000000000, 0.000000000000000000, 5.000000000000000000 ) ) ;
#75417=ADVANCED_FACE ( 'NONE', ( #143349 ), #96948, .F. ) ;
#75418=VECTOR ( 'NONE', #62091, 1000.000000000000227 ) ;
#75420=ORIENTED_EDGE ( 'NONE', *, *, #89947, .T. ) ;
#75422=EDGE_CURVE ( 'NONE', #23928, #49613, #140487, .T. ) ;
#75423=LINE ( 'NONE', #76875, #12342 ) ;
#75424=VERTEX_POINT ( 'NONE', #131776 ) ;
#75425=CARTESIAN_POINT ( 'NONE',  ( -0.4892135623730947680, -27.52281430457055578, 5.000000000000000000 ) ) ;
#75426=ORIENTED_EDGE ( 'NONE', *, *, #23885, .T. ) ;
#75428=LINE ( 'NONE', #7272, #35427 ) ;
#75429=CARTESIAN_POINT ( 'NONE',  ( 78.48921356237309510, -27.52281430457109934, 5.000000000000000000 ) ) ;
#75430=ADVANCED_FACE ( 'NONE', ( #65108 ), #85387, .F. ) ;
#75431=VERTEX_POINT ( 'NONE', #41917 ) ;
#75432=DIRECTION ( 'NONE',  ( 0.7071067811865487940, -0.7071067811865463515, 0.000000000000000000 ) ) ;
#75434=CARTESIAN_POINT ( 'NONE',  ( 23.99451991528749062, 28.92564299267954908, 4.000000000000000000 ) ) ;
#75435=VECTOR ( 'NONE', #135752, 1000.000000000000000 ) ;
#75436=VECTOR ( 'NONE', #116016, 1000.000000000000227 ) ;
#75437=CARTESIAN_POINT ( 'NONE',  ( 0.000000000000000000, 0.000000000000000000, 5.000000000000000000 ) ) ;
#75439=PLANE ( 'NONE',  #46740 ) ;
#75440=CARTESIAN_POINT ( 'NONE',  ( -34.26506670282030598, 12.75929247661558996, 18.34774599283964136 ) ) ;
#75441=EDGE_CURVE ( 'NONE', #143132, #133910, #32466, .T. ) ;
#75442=PLANE ( 'NONE',  #13639 ) ;
#75443=CARTESIAN_POINT ( 'NONE',  ( -69.29974487139159578, -27.71228299555254537, 4.000000000000000000 ) ) ;
#75444=DIRECTION ( 'NONE',  ( 0.6830127018922181881, 0.6830127018922202975, -0.2588190451025214056 ) ) ;
#75445=LINE ( 'NONE', #8008, #117719 ) ;
#75446=AXIS2_PLACEMENT_3D ( 'NONE', #129602, #119424, #132518 ) ;
#75447=CARTESIAN_POINT ( 'NONE',  ( 29.99999999999979039, 7.588810512006244124, -3.013526669885294496 ) ) ;
#75448=CARTESIAN_POINT ( 'NONE',  ( -11.51078643762690490, -27.52281430457047406, 5.000000000000000000 ) ) ;
#75449=ORIENTED_EDGE ( 'NONE', *, *, #25073, .F. ) ;
#75450=ORIENTED_EDGE ( 'NONE', *, *, #33830, .T. ) ;
#75452=EDGE_CURVE ( 'NONE', #120532, #34652, #86126, .T. ) ;
#75454=ORIENTED_EDGE ( 'NONE', *, *, #107044, .F. ) ;
#75455=ORIENTED_EDGE ( 'NONE', *, *, #65994, .F. ) ;
#75456=EDGE_CURVE ( 'NONE', #78816, #2171, #120134, .T. ) ;
#75457=ORIENTED_EDGE ( 'NONE', *, *, #8443, .F. ) ;
#75458=FACE_OUTER_BOUND ( 'NONE', #12185, .T. ) ;
#75459=DIRECTION ( 'NONE',  ( -0.7071067811865486830, 0.7071067811865464625, 0.000000000000000000 ) ) ;
#75460=ORIENTED_EDGE ( 'NONE', *, *, #58757, .F. ) ;
#75462=EDGE_CURVE ( 'NONE', #46985, #117324, #89684, .T. ) ;
#75463=DIRECTION ( 'NONE',  ( -0.3543493200069162685, -0.000000000000000000, -0.9351131265310288487 ) ) ;
#75464=DIRECTION ( 'NONE',  ( -0.7071067811865486830, -0.7071067811865464625, 0.000000000000000000 ) ) ;
#75465=CARTESIAN_POINT ( 'NONE',  ( 34.42499999999998295, 22.22500000000000142, 5.000000000000000000 ) ) ;
#75467=ORIENTED_EDGE ( 'NONE', *, *, #115859, .T. ) ;
#75470=CARTESIAN_POINT ( 'NONE',  ( 20.81601139373100295, 28.73617430169773002, 5.000000000000000000 ) ) ;
#75471=DIRECTION ( 'NONE',  ( -0.7071067811865486830, -0.7071067811865464625, 0.000000000000000000 ) ) ;
#75472=DIRECTION ( 'NONE',  ( 0.7071067811865487940, 0.7071067811865463515, 0.000000000000000000 ) ) ;
#75473=DIRECTION ( 'NONE',  ( 0.6830127018922180770, -0.6830127018922204085, -0.2588190451025213501 ) ) ;
#75476=ORIENTED_EDGE ( 'NONE', *, *, #66124, .F. ) ;
#75477=ORIENTED_EDGE ( 'NONE', *, *, #9165, .F. ) ;
#75479=ORIENTED_EDGE ( 'NONE', *, *, #62909, .F. ) ;
#75480=EDGE_CURVE ( 'NONE', #95062, #16368, #69383, .T. ) ;
#75482=DIRECTION ( 'NONE',  ( -0.000000000000000000, 1.000000000000000000, -0.000000000000000000 ) ) ;
#75483=CARTESIAN_POINT ( 'NONE',  ( 14.99999999999991296, 20.58746187583903620, 4.000000000000000000 ) ) ;
#75485=CARTESIAN_POINT ( 'NONE',  ( -11.81601139373100651, 28.73617430169779041, 5.000000000000000000 ) ) ;
#75487=ORIENTED_EDGE ( 'NONE', *, *, #101551, .F. ) ;
#75488=CARTESIAN_POINT ( 'NONE',  ( 18.48921356237309510, -27.52281430457068367, 5.000000000000000000 ) ) ;
#75489=VERTEX_POINT ( 'NONE', #133911 ) ;
#75490=CARTESIAN_POINT ( 'NONE',  ( -27.48921356237309155, -27.52281430457074762, 5.000000000000000000 ) ) ;
#75491=CARTESIAN_POINT ( 'NONE',  ( -2.994519915287485734, 28.92564299267940342, 4.000000000000000000 ) ) ;
#75492=DIRECTION ( 'NONE',  ( -0.7071067811865486830, -0.7071067811865464625, -0.000000000000000000 ) ) ;
#75493=FACE_OUTER_BOUND ( 'NONE', #84141, .T. ) ;
#75494=ORIENTED_EDGE ( 'NONE', *, *, #122900, .F. ) ;
#75495=EDGE_CURVE ( 'NONE', #47009, #88720, #88996, .T. ) ;
#75497=EDGE_LOOP ( 'NONE', ( #79750, #110260, #20933, #104327 ) ) ;
#75498=LINE ( 'NONE', #63231, #5401 ) ;
#75499=CARTESIAN_POINT ( 'NONE',  ( 17.99451991528748351, 28.92564299267950645, 4.000000000000000000 ) ) ;
#75501=CARTESIAN_POINT ( 'NONE',  ( 26.99999999999980815, 11.58746187583913390, 4.000000000000000000 ) ) ;
#75502=VECTOR ( 'NONE', #51976, 1000.000000000000000 ) ;
#75503=EDGE_CURVE ( 'NONE', #67140, #13632, #136044, .T. ) ;
#75505=ORIENTED_EDGE ( 'NONE', *, *, #53404, .F. ) ;
#75506=AXIS2_PLACEMENT_3D ( 'NONE', #72512, #105772, #140561 ) ;
#75507=CARTESIAN_POINT ( 'NONE',  ( 34.42499999999998295, -4.458600742197917910, 5.000000000000000000 ) ) ;
#75509=ORIENTED_EDGE ( 'NONE', *, *, #78533, .T. ) ;
#75510=ORIENTED_EDGE ( 'NONE', *, *, #13181, .T. ) ;
#75512=ADVANCED_FACE ( 'NONE', ( #113568 ), #12112, .F. ) ;
#75514=VERTEX_POINT ( 'NONE', #110688 ) ;
#75515=CARTESIAN_POINT ( 'NONE',  ( -34.45011844616454511, 6.002304141593897135, 5.000000000000000888 ) ) ;
#75517=PLANE ( 'NONE',  #43303 ) ;
#75518=DIRECTION ( 'NONE',  ( 0.7071067811865486830, -0.7071067811865464625, -0.000000000000000000 ) ) ;
#75519=DIRECTION ( 'NONE',  ( 0.7071067811865487940, -0.7071067811865463515, 0.000000000000000000 ) ) ;
#75520=AXIS2_PLACEMENT_3D ( 'NONE', #46280, #59298, #70186 ) ;
#75521=FACE_BOUND ( 'NONE', #124885, .T. ) ;
#75522=ORIENTED_EDGE ( 'NONE', *, *, #37126, .T. ) ;
#75523=EDGE_CURVE ( 'NONE', #16561, #96125, #91144, .T. ) ;
#75524=LINE ( 'NONE', #6636, #66499 ) ;
#75525=DIRECTION ( 'NONE',  ( 0.7071067811865486830, -0.7071067811865464625, -0.000000000000000000 ) ) ;
#75526=CARTESIAN_POINT ( 'NONE',  ( 6.707106781186498168, 17.25929247661554911, 5.000000000000000000 ) ) ;
#75527=ORIENTED_EDGE ( 'NONE', *, *, #50898, .F. ) ;
#75528=CARTESIAN_POINT ( 'NONE',  ( -44.99451991528749772, 28.92564299267969474, 4.000000000000000000 ) ) ;
#75529=ORIENTED_EDGE ( 'NONE', *, *, #91601, .F. ) ;
#75531=DIRECTION ( 'NONE',  ( 0.6830127018922180770, -0.6830127018922204085, -0.2588190451025213501 ) ) ;
#75532=AXIS2_PLACEMENT_3D ( 'NONE', #26986, #125613, #105262 ) ;
#75533=ORIENTED_EDGE ( 'NONE', *, *, #112209, .F. ) ;
#75534=VECTOR ( 'NONE', #9681, 1000.000000000000000 ) ;
#75535=AXIS2_PLACEMENT_3D ( 'NONE', #68192, #112366, #13022 ) ;
#75538=DIRECTION ( 'NONE',  ( -0.000000000000000000, 0.3543493200069153248, 0.9351131265310292928 ) ) ;
#75539=VERTEX_POINT ( 'NONE', #101995 ) ;
#75540=VECTOR ( 'NONE', #117334, 1000.000000000000000 ) ;
#75541=CARTESIAN_POINT ( 'NONE',  ( -12.15612307739231923, -22.22499999999999432, 4.000000000000000000 ) ) ;
#75542=ORIENTED_EDGE ( 'NONE', *, *, #95009, .T. ) ;
#75543=DIRECTION ( 'NONE',  ( 0.7071067811865487940, 0.7071067811865463515, 0.000000000000000000 ) ) ;
#75545=AXIS2_PLACEMENT_3D ( 'NONE', #102200, #24617, #35543 ) ;
#75546=LINE ( 'NONE', #119719, #57205 ) ;
#75548=CARTESIAN_POINT ( 'NONE',  ( 10.49999999999992184, 22.01701374228156283, 2.453858888625607193 ) ) ;
#75549=PLANE ( 'NONE',  #137380 ) ;
#75550=PLANE ( 'NONE',  #57947 ) ;
#75551=ORIENTED_EDGE ( 'NONE', *, *, #28033, .T. ) ;
#75553=ORIENTED_EDGE ( 'NONE', *, *, #92454, .T. ) ;
#75554=EDGE_LOOP ( 'NONE', ( #50301, #15263, #64861, #46150 ) ) ;
#75555=CARTESIAN_POINT ( 'NONE',  ( -27.79333936457828358, 21.75929247661549581, 4.998822639870701856 ) ) ;
#75556=LINE ( 'NONE', #16889, #141623 ) ;
#75557=ORIENTED_EDGE ( 'NONE', *, *, #105987, .T. ) ;
#75558=ADVANCED_FACE ( 'NONE', ( #25857 ), #11369, .T. ) ;
#75560=DIRECTION ( 'NONE',  ( 0.6830127018922181881, 0.6830127018922202975, -0.2588190451025214056 ) ) ;
#75561=DIRECTION ( 'NONE',  ( 0.7071067811865487940, -0.7071067811865463515, 0.000000000000000000 ) ) ;
#75562=EDGE_CURVE ( 'NONE', #45356, #139610, #111431, .T. ) ;
#75563=ADVANCED_FACE ( 'NONE', ( #45506 ), #104101, .F. ) ;
#75564=CARTESIAN_POINT ( 'NONE',  ( 17.91508676806227029, -12.74070752338415247, 18.74364270924358422 ) ) ;
#75566=CARTESIAN_POINT ( 'NONE',  ( 9.183988606268997046, 28.73617430169793607, 5.000000000000000000 ) ) ;
#75568=ADVANCED_FACE ( 'NONE', ( #16380 ), #17128, .T. ) ;
#75569=EDGE_CURVE ( 'NONE', #26874, #59437, #128739, .T. ) ;
#75571=CARTESIAN_POINT ( 'NONE',  ( -24.18398860626899705, 28.73617430169804265, 5.000000000000000000 ) ) ;
#75572=ADVANCED_FACE ( 'NONE', ( #126579 ), #70130, .F. ) ;
#75573=ORIENTED_EDGE ( 'NONE', *, *, #29371, .T. ) ;
#75575=EDGE_CURVE ( 'NONE', #108859, #125764, #93256, .T. ) ;
#75576=DIRECTION ( 'NONE',  ( -0.7071067811865486830, -0.7071067811865464625, -0.000000000000000000 ) ) ;
#75577=CARTESIAN_POINT ( 'NONE',  ( -34.92500000000001137, -5.993876922608009750, 4.000000000000000000 ) ) ;
#75578=CARTESIAN_POINT ( 'NONE',  ( 15.70710678118643955, 11.25929247661560950, 5.000000000000000000 ) ) ;
#75579=ORIENTED_EDGE ( 'NONE', *, *, #12955, .F. ) ;
#75580=AXIS2_PLACEMENT_3D ( 'NONE', #50502, #6938, #17834 ) ;
#75582=ORIENTED_EDGE ( 'NONE', *, *, #40066, .F. ) ;
#75583=ADVANCED_FACE ( 'NONE', ( #72978 ), #114290, .T. ) ;
#75584=DIRECTION ( 'NONE',  ( -0.7071067811865486830, -0.7071067811865464625, 0.000000000000000000 ) ) ;
#75586=LINE ( 'NONE', #119755, #44935 ) ;
#75587=ORIENTED_EDGE ( 'NONE', *, *, #56967, .F. ) ;
#75588=EDGE_CURVE ( 'NONE', #98816, #113076, #115679, .T. ) ;
#75590=CARTESIAN_POINT ( 'NONE',  ( -23.47599861414534672, 22.03583458319436872, 4.979811245910092055 ) ) ;
#75591=VECTOR ( 'NONE', #59076, 1000.000000000000000 ) ;
#75592=VERTEX_POINT ( 'NONE', #136750 ) ;
#75593=CARTESIAN_POINT ( 'NONE',  ( -27.18398860626900060, 28.73617430169806042, 5.000000000000000000 ) ) ;
#75594=DIRECTION ( 'NONE',  ( 0.7071067811865486830, -0.7071067811865464625, -0.000000000000000000 ) ) ;
#75595=ORIENTED_EDGE ( 'NONE', *, *, #50395, .T. ) ;
#75596=EDGE_CURVE ( 'NONE', #85671, #18530, #50479, .T. ) ;
#75597=CARTESIAN_POINT ( 'NONE',  ( -5.916851932270658310, 21.75929247661548871, 7.311836541448040627 ) ) ;
#75598=CARTESIAN_POINT ( 'NONE',  ( 27.48921356237309155, -27.52281430457074762, 5.000000000000000000 ) ) ;
#75599=ORIENTED_EDGE ( 'NONE', *, *, #135676, .F. ) ;
#75600=ORIENTED_EDGE ( 'NONE', *, *, #77714, .F. ) ;
#75601=CARTESIAN_POINT ( 'NONE',  ( 72.29974487139158157, -27.71228299555256669, 4.000000000000000000 ) ) ;
#75602=CARTESIAN_POINT ( 'NONE',  ( 0.3281693992235289459, -0.7407075233842805861, 4.000000000000000000 ) ) ;
#75603=EDGE_CURVE ( 'NONE', #49858, #1646, #4042, .T. ) ;
#75605=CARTESIAN_POINT ( 'NONE',  ( 19.05000000000000071, 3.174999999999997158, 4.000000000000000000 ) ) ;
#75606=PLANE ( 'NONE',  #64649 ) ;
#75607=CARTESIAN_POINT ( 'NONE',  ( 18.18398860626898994, 28.73617430169800002, 5.000000000000000000 ) ) ;
#75609=VERTEX_POINT ( 'NONE', #83103 ) ;
#75610=DIRECTION ( 'NONE',  ( 0.7071067811865486830, -0.7071067811865463515, 0.000000000000000000 ) ) ;
#75611=LINE ( 'NONE', #119785, #97967 ) ;
#75614=CARTESIAN_POINT ( 'NONE',  ( -17.67183060077634593, -18.74070752338409207, 4.000000000000000000 ) ) ;
#75615=VERTEX_POINT ( 'NONE', #83850 ) ;
#75616=ORIENTED_EDGE ( 'NONE', *, *, #141851, .T. ) ;
#75617=EDGE_CURVE ( 'NONE', #55039, #67716, #6914, .T. ) ;
#75618=DIRECTION ( 'NONE',  ( -0.000000000000000000, 0.3543493200069153248, 0.9351131265310292928 ) ) ;
#75619=ORIENTED_EDGE ( 'NONE', *, *, #91372, .T. ) ;
#75620=VECTOR ( 'NONE', #16464, 1000.000000000000227 ) ;
#75621=EDGE_CURVE ( 'NONE', #85320, #52679, #138922, .T. ) ;
#75622=ORIENTED_EDGE ( 'NONE', *, *, #40849, .F. ) ;
#75623=CARTESIAN_POINT ( 'NONE',  ( 29.99999999999980105, -4.447814304570781196, 5.000000000000000000 ) ) ;
#75624=FACE_OUTER_BOUND ( 'NONE', #124777, .T. ) ;
#75626=EDGE_CURVE ( 'NONE', #12371, #80353, #48329, .T. ) ;
#75627=DIRECTION ( 'NONE',  ( 0.7071067811865486830, -0.7071067811865464625, -0.000000000000000000 ) ) ;
#75628=CARTESIAN_POINT ( 'NONE',  ( 8.501836514860380944, -17.24070752338410628, 8.407044977365202953 ) ) ;
#75629=LINE ( 'NONE', #118389, #83432 ) ;
#75631=LINE ( 'NONE', #64747, #114799 ) ;
#75632=ORIENTED_EDGE ( 'NONE', *, *, #45824, .T. ) ;
#75633=DIRECTION ( 'NONE',  ( 0.3543493200069162685, -0.000000000000000000, -0.9351131265310288487 ) ) ;
#75634=LINE ( 'NONE', #40858, #547 ) ;
#75637=CARTESIAN_POINT ( 'NONE',  ( 0.000000000000000000, 0.000000000000000000, 5.000000000000000000 ) ) ;
#75639=DIRECTION ( 'NONE',  ( 0.7071067811865487940, 0.7071067811865463515, 0.000000000000000000 ) ) ;
#75640=PLANE ( 'NONE',  #6414 ) ;
#75641=AXIS2_PLACEMENT_3D ( 'NONE', #23976, #124708, #46486 ) ;
#75643=VECTOR ( 'NONE', #13927, 1000.000000000000000 ) ;
#75644=LINE ( 'NONE', #64761, #120192 ) ;
#75645=ORIENTED_EDGE ( 'NONE', *, *, #61697, .F. ) ;
#75648=LINE ( 'NONE', #13029, #16980 ) ;
#75649=ADVANCED_FACE ( 'NONE', ( #28008 ), #15647, .F. ) ;
#75650=DIRECTION ( 'NONE',  ( 0.7071067811865487940, 0.7071067811865463515, 0.000000000000000000 ) ) ;
#75651=CARTESIAN_POINT ( 'NONE',  ( -21.70701326429289324, -21.74070752338406010, 4.999753212805221558 ) ) ;
#75652=ORIENTED_EDGE ( 'NONE', *, *, #28168, .F. ) ;
#75653=DIRECTION ( 'NONE',  ( -0.7071067811865487940, 0.7071067811865463515, 0.000000000000000000 ) ) ;
#75654=CARTESIAN_POINT ( 'NONE',  ( 13.24976746729824129, 4.588264127556670680, 4.661243073242808066 ) ) ;
#75658=ORIENTED_EDGE ( 'NONE', *, *, #137782, .F. ) ;
#75661=CARTESIAN_POINT ( 'NONE',  ( -1.396568071053559734, -14.24070752338413648, 19.24067776001725960 ) ) ;
#75662=DIRECTION ( 'NONE',  ( 0.000000000000000000, -1.000000000000000000, 0.000000000000000000 ) ) ;
#75663=CARTESIAN_POINT ( 'NONE',  ( 16.99806943317890529, -22.22500000000000142, 4.500000000000000888 ) ) ;
#75665=EDGE_CURVE ( 'NONE', #35917, #73867, #76735, .T. ) ;
#75668=ORIENTED_EDGE ( 'NONE', *, *, #45645, .T. ) ;
#75671=FACE_OUTER_BOUND ( 'NONE', #24898, .T. ) ;
#75672=CARTESIAN_POINT ( 'NONE',  ( 34.92499999999998295, -21.72500000000000142, 5.000000000000000000 ) ) ;
#75673=CARTESIAN_POINT ( 'NONE',  ( -33.32816939922328459, 20.25929247661552779, 4.000000000000000000 ) ) ;
#75674=CARTESIAN_POINT ( 'NONE',  ( -34.17183060077623225, -17.24070752338410983, 4.000000000000000000 ) ) ;
#75676=VERTEX_POINT ( 'NONE', #62083 ) ;
#75677=AXIS2_PLACEMENT_3D ( 'NONE', #121712, #110822, #57225 ) ;
#75678=FACE_OUTER_BOUND ( 'NONE', #130412, .T. ) ;
#75680=DIRECTION ( 'NONE',  ( -0.3543493200069162685, -0.000000000000000000, -0.9351131265310288487 ) ) ;
#75681=CARTESIAN_POINT ( 'NONE',  ( -28.00193056682078918, -22.22500000000000142, 4.500000000000000888 ) ) ;
#75682=DIRECTION ( 'NONE',  ( 0.7071067811865487940, -0.7071067811865463515, 0.000000000000000000 ) ) ;
#75683=VERTEX_POINT ( 'NONE', #95396 ) ;
#75684=EDGE_LOOP ( 'NONE', ( #96101, #86080, #85590, #142193 ) ) ;
#75685=VECTOR ( 'NONE', #116653, 1000.000000000000227 ) ;
#75686=DIRECTION ( 'NONE',  ( 0.7071067811865487940, 0.7071067811865463515, 0.000000000000000000 ) ) ;
#75687=ORIENTED_EDGE ( 'NONE', *, *, #90380, .T. ) ;
#75689=VERTEX_POINT ( 'NONE', #120704 ) ;
#75690=ADVANCED_FACE ( 'NONE', ( #130913 ), #141035, .F. ) ;
#75691=CARTESIAN_POINT ( 'NONE',  ( 28.49999999999980460, 22.01701374228157704, 2.453858888625564560 ) ) ;
#75692=EDGE_LOOP ( 'NONE', ( #12018, #15001, #139369, #16727, #126242, #115717 ) ) ;
#75693=LINE ( 'NONE', #131498, #86253 ) ;
#75694=LINE ( 'NONE', #18408, #108083 ) ;
#75695=AXIS2_PLACEMENT_3D ( 'NONE', #32108, #99473, #55302 ) ;
#75696=CARTESIAN_POINT ( 'NONE',  ( 39.48921356237310221, -27.52281430457082934, 5.000000000000000000 ) ) ;
#75697=VECTOR ( 'NONE', #83365, 1000.000000000000227 ) ;
#75698=FACE_BOUND ( 'NONE', #32676, .T. ) ;
#75699=EDGE_CURVE ( 'NONE', #41122, #128067, #41740, .T. ) ;
#75700=FACE_OUTER_BOUND ( 'NONE', #78602, .T. ) ;
#75701=CARTESIAN_POINT ( 'NONE',  ( -21.96495920677946856, -2.033836129387410985, 4.000000000000000000 ) ) ;
#75702=LINE ( 'NONE', #140931, #1686 ) ;
#75705=CARTESIAN_POINT ( 'NONE',  ( 14.81601139373099585, 28.73617430169776910, 5.000000000000000000 ) ) ;
#75708=VERTEX_POINT ( 'NONE', #53313 ) ;
#75709=EDGE_LOOP ( 'NONE', ( #31171, #7179, #117223, #21202 ) ) ;
#75711=VERTEX_POINT ( 'NONE', #98268 ) ;
#75712=CARTESIAN_POINT ( 'NONE',  ( -23.29298673570678702, -21.74070752338405299, 4.999753212805217117 ) ) ;
#75713=CARTESIAN_POINT ( 'NONE',  ( -5.816011393731002066, 28.73617430169783304, 5.000000000000000000 ) ) ;
#75714=VERTEX_POINT ( 'NONE', #87395 ) ;
#75717=LINE ( 'NONE', #8962, #120056 ) ;
#75719=PLANE ( 'NONE',  #1850 ) ;
#75720=CARTESIAN_POINT ( 'NONE',  ( -28.82816939922332722, -2.240707523384255939, 4.000000000000000000 ) ) ;
#75723=EDGE_LOOP ( 'NONE', ( #9055, #136149, #114252, #137324 ) ) ;
#75725=VERTEX_POINT ( 'NONE', #98951 ) ;
#75726=CARTESIAN_POINT ( 'NONE',  ( -7.171830600776418763, -2.240707523384260824, 4.000000000000000000 ) ) ;
#75727=DIRECTION ( 'NONE',  ( -0.7071067811865486830, -0.7071067811865464625, 0.000000000000000000 ) ) ;
#75728=ORIENTED_EDGE ( 'NONE', *, *, #135977, .F. ) ;
#75729=AXIS2_PLACEMENT_3D ( 'NONE', #66598, #121656, #33289 ) ;
#75730=ORIENTED_EDGE ( 'NONE', *, *, #142204, .T. ) ;
#75733=EDGE_LOOP ( 'NONE', ( #66839, #81636, #128340, #18132 ) ) ;
#75735=AXIS2_PLACEMENT_3D ( 'NONE', #140922, #141667, #119175 ) ;
#75736=VECTOR ( 'NONE', #9491, 1000.000000000000000 ) ;
#75737=FACE_OUTER_BOUND ( 'NONE', #128792, .T. ) ;
#75739=EDGE_CURVE ( 'NONE', #115165, #136354, #74387, .T. ) ;
#75742=EDGE_CURVE ( 'NONE', #38188, #65156, #31584, .T. ) ;
#75743=ORIENTED_EDGE ( 'NONE', *, *, #103956, .F. ) ;
#75745=EDGE_CURVE ( 'NONE', #80320, #50236, #75807, .T. ) ;
#75746=ORIENTED_EDGE ( 'NONE', *, *, #129757, .T. ) ;
#75748=VECTOR ( 'NONE', #32140, 999.9999999999998863 ) ;
#75749=FACE_OUTER_BOUND ( 'NONE', #132379, .T. ) ;
#75750=DIRECTION ( 'NONE',  ( 0.7071067811865487940, 0.7071067811865463515, 0.000000000000000000 ) ) ;
#75751=ORIENTED_EDGE ( 'NONE', *, *, #84508, .T. ) ;
#75752=ORIENTED_EDGE ( 'NONE', *, *, #32747, .F. ) ;
#75753=EDGE_CURVE ( 'NONE', #94242, #6978, #141784, .T. ) ;
#75754=FACE_OUTER_BOUND ( 'NONE', #35996, .T. ) ;
#75755=DIRECTION ( 'NONE',  ( -0.000000000000000000, -0.3543493200069152693, 0.9351131265310292928 ) ) ;
#75756=CARTESIAN_POINT ( 'NONE',  ( 8.994519915287490619, 28.92564299267944250, 4.000000000000000000 ) ) ;
#75757=ORIENTED_EDGE ( 'NONE', *, *, #101040, .T. ) ;
#75758=CARTESIAN_POINT ( 'NONE',  ( 12.48921356237309155, -27.52281430457064104, 5.000000000000000000 ) ) ;
#75759=ORIENTED_EDGE ( 'NONE', *, *, #62584, .T. ) ;
#75760=EDGE_LOOP ( 'NONE', ( #23891, #2224, #139022, #87116 ) ) ;
#75761=VERTEX_POINT ( 'NONE', #41021 ) ;
#75762=EDGE_CURVE ( 'NONE', #23165, #78911, #85955, .T. ) ;
#75764=CARTESIAN_POINT ( 'NONE',  ( -14.99999999999989875, 7.931123077392104648, 4.000000000000000000 ) ) ;
#75765=CARTESIAN_POINT ( 'NONE',  ( 34.92499999999998295, 22.22500000000000142, 4.000000000000000000 ) ) ;
#75766=DIRECTION ( 'NONE',  ( -0.000000000000000000, -0.3543493200069152693, 0.9351131265310292928 ) ) ;
#75767=DIRECTION ( 'NONE',  ( 0.7071067811865487940, 0.7071067811865463515, -0.000000000000000000 ) ) ;
#75768=EDGE_CURVE ( 'NONE', #16920, #33497, #91538, .T. ) ;
#75769=CARTESIAN_POINT ( 'NONE',  ( -18.32816939922339117, -18.74070752338409562, 4.000000000000000000 ) ) ;
#75770=CARTESIAN_POINT ( 'NONE',  ( 9.489213562373095101, -27.52281430457062328, 5.000000000000000000 ) ) ;
#75771=EDGE_CURVE ( 'NONE', #54960, #81537, #10511, .T. ) ;
#75773=DIRECTION ( 'NONE',  ( -0.6830127018922180770, -0.6830127018922204085, -0.2588190451025213501 ) ) ;
#75774=ORIENTED_EDGE ( 'NONE', *, *, #68172, .T. ) ;
#75775=AXIS2_PLACEMENT_3D ( 'NONE', #34918, #67561, #3649 ) ;
#75776=LINE ( 'NONE', #109815, #88804 ) ;
#75777=EDGE_CURVE ( 'NONE', #5899, #66460, #129449, .T. ) ;
#75778=CARTESIAN_POINT ( 'NONE',  ( -63.18398860626900415, 28.73617430169831621, 5.000000000000000000 ) ) ;
#75779=VECTOR ( 'NONE', #69264, 1000.000000000000000 ) ;
#75780=ORIENTED_EDGE ( 'NONE', *, *, #114096, .T. ) ;
#75781=LINE ( 'NONE', #86660, #4328 ) ;
#75782=LINE ( 'NONE', #85924, #67539 ) ;
#75783=ORIENTED_EDGE ( 'NONE', *, *, #138887, .T. ) ;
#75785=DIRECTION ( 'NONE',  ( -0.7071067811865487940, 0.7071067811865463515, -0.000000000000000000 ) ) ;
#75786=CARTESIAN_POINT ( 'NONE',  ( -24.18398860626899705, 28.73617430169804265, 5.000000000000000000 ) ) ;
#75787=CARTESIAN_POINT ( 'NONE',  ( 26.24139925780185578, 21.72500000000000142, 5.000000000000000000 ) ) ;
#75789=FACE_OUTER_BOUND ( 'NONE', #12857, .T. ) ;
#75791=LINE ( 'NONE', #107677, #30197 ) ;
#75792=CARTESIAN_POINT ( 'NONE',  ( 5.999999999999954703, 7.931123077392102871, 4.000000000000000000 ) ) ;
#75794=LINE ( 'NONE', #65671, #25589 ) ;
#75796=CARTESIAN_POINT ( 'NONE',  ( -32.99999999999976552, 11.96639925780213431, 5.000000000000000000 ) ) ;
#75797=EDGE_CURVE ( 'NONE', #26207, #4325, #21418, .T. ) ;
#75798=VECTOR ( 'NONE', #62998, 1000.000000000000000 ) ;
#75799=VERTEX_POINT ( 'NONE', #63528 ) ;
#75800=LINE ( 'NONE', #119961, #6095 ) ;
#75801=DIRECTION ( 'NONE',  ( -0.6830127018922180770, -0.6830127018922204085, -0.2588190451025213501 ) ) ;
#75802=VERTEX_POINT ( 'NONE', #18519 ) ;
#75803=LINE ( 'NONE', #119966, #110898 ) ;
#75804=DIRECTION ( 'NONE',  ( 0.7071067811865487940, 0.7071067811865463515, 0.000000000000000000 ) ) ;
#75805=ORIENTED_EDGE ( 'NONE', *, *, #57280, .T. ) ;
#75806=DIRECTION ( 'NONE',  ( -0.000000000000000000, 0.000000000000000000, 1.000000000000000000 ) ) ;
#75807=LINE ( 'NONE', #119972, #71880 ) ;
#75809=ORIENTED_EDGE ( 'NONE', *, *, #6575, .F. ) ;
#75810=ORIENTED_EDGE ( 'NONE', *, *, #68796, .T. ) ;
#75812=LINE ( 'NONE', #29423, #7374 ) ;
#75813=DIRECTION ( 'NONE',  ( 0.7071067811865486830, -0.7071067811865464625, -0.000000000000000000 ) ) ;
#75814=ADVANCED_FACE ( 'NONE', ( #140336 ), #62801, .F. ) ;
#75817=FACE_OUTER_BOUND ( 'NONE', #116373, .T. ) ;
#75818=CARTESIAN_POINT ( 'NONE',  ( 34.49999999999975842, -10.53574439159940113, 4.994342998332163219 ) ) ;
#75819=ORIENTED_EDGE ( 'NONE', *, *, #117266, .F. ) ;
#75820=VECTOR ( 'NONE', #76978, 1000.000000000000000 ) ;
#75821=CARTESIAN_POINT ( 'NONE',  ( 3.489213562373097322, -27.52281430457057709, 5.000000000000000000 ) ) ;
#75822=EDGE_CURVE ( 'NONE', #97989, #4786, #39483, .T. ) ;
#75824=CARTESIAN_POINT ( 'NONE',  ( -31.17183060077625001, 15.75929247661555443, 4.000000000000000000 ) ) ;
#75826=DIRECTION ( 'NONE',  ( -0.000000000000000000, 0.3543493200069153248, 0.9351131265310292928 ) ) ;
#75828=ADVANCED_FACE ( 'NONE', ( #30133 ), #107692, .F. ) ;
#75830=LINE ( 'NONE', #84569, #29199 ) ;
#75831=DIRECTION ( 'NONE',  ( 1.000000000000000000, 0.000000000000000000, 0.000000000000000000 ) ) ;
#75832=EDGE_LOOP ( 'NONE', ( #88250, #23229, #91821, #5142 ) ) ;
#75834=VECTOR ( 'NONE', #57760, 1000.000000000000227 ) ;
#75835=CARTESIAN_POINT ( 'NONE',  ( 20.99451991528748707, 28.92564299267952777, 4.000000000000000000 ) ) ;
#75837=DIRECTION ( 'NONE',  ( -0.3543493200069162685, -0.000000000000000000, -0.9351131265310288487 ) ) ;
#75838=EDGE_CURVE ( 'NONE', #40937, #102057, #109125, .T. ) ;
#75839=CARTESIAN_POINT ( 'NONE',  ( 23.51078643762690490, -27.52281430457038880, 5.000000000000000000 ) ) ;
#75840=CARTESIAN_POINT ( 'NONE',  ( 32.99999999999977973, -9.033600742197641864, 5.000000000000000000 ) ) ;
#75842=DIRECTION ( 'NONE',  ( 0.7071067811865487940, -0.7071067811865463515, 0.000000000000000000 ) ) ;
#75843=LINE ( 'NONE', #20719, #107785 ) ;
#75844=DIRECTION ( 'NONE',  ( -0.3543493200069162685, -0.000000000000000000, -0.9351131265310288487 ) ) ;
#75846=VECTOR ( 'NONE', #230, 1000.000000000000000 ) ;
#75849=AXIS2_PLACEMENT_3D ( 'NONE', #41965, #86180, #99158 ) ;
#75851=ORIENTED_EDGE ( 'NONE', *, *, #80367, .F. ) ;
#75852=PLANE ( 'NONE',  #5918 ) ;
#75853=LINE ( 'NONE', #32344, #122116 ) ;
#75854=VECTOR ( 'NONE', #63577, 1000.000000000000000 ) ;
#75856=ORIENTED_EDGE ( 'NONE', *, *, #143083, .F. ) ;
#75857=CARTESIAN_POINT ( 'NONE',  ( -15.48921356237309510, -27.52281430457066236, 5.000000000000000000 ) ) ;
#75859=EDGE_LOOP ( 'NONE', ( #74709, #45834, #62314, #67976 ) ) ;
#75860=EDGE_CURVE ( 'NONE', #33966, #112760, #109883, .T. ) ;
#75861=LINE ( 'NONE', #96845, #32921 ) ;
#75863=DIRECTION ( 'NONE',  ( 0.6830127018922181881, 0.6830127018922202975, -0.2588190451025214056 ) ) ;
#75864=( BOUNDED_CURVE ( )  B_SPLINE_CURVE ( 3, ( #68199, #101479, #78320, #110904 ),
 .UNSPECIFIED., .F., .T. ) 
 B_SPLINE_CURVE_WITH_KNOTS ( ( 4, 4 ),
 ( 5.536208752217765650, 5.573248253235211891 ),
 .UNSPECIFIED. ) 
 CURVE ( )  GEOMETRIC_REPRESENTATION_ITEM ( )  RATIONAL_B_SPLINE_CURVE ( ( 1.000000000000000000, 0.9998856762146628441, 0.9998856762146628441, 1.000000000000000000 ) ) 
 REPRESENTATION_ITEM ( '' )  );
#75865=VERTEX_POINT ( 'NONE', #44641 ) ;
#75866=EDGE_LOOP ( 'NONE', ( #55562, #12336, #42954, #112297 ) ) ;
#75867=EDGE_CURVE ( 'NONE', #37645, #39717, #11202, .T. ) ;
#75868=FACE_BOUND ( 'NONE', #111474, .T. ) ;
#75869=EDGE_CURVE ( 'NONE', #131124, #126973, #79416, .T. ) ;
#75870=CARTESIAN_POINT ( 'NONE',  ( -23.81601139373100295, 28.73617430169770870, 5.000000000000000000 ) ) ;
#75871=DIRECTION ( 'NONE',  ( -0.7071067811865486830, -0.7071067811865464625, -0.000000000000000000 ) ) ;
#75873=CARTESIAN_POINT ( 'NONE',  ( 0.000000000000000000, 0.000000000000000000, 5.000000000000000000 ) ) ;
#75874=CARTESIAN_POINT ( 'NONE',  ( 42.48921356237308800, -27.52281430457085065, 5.000000000000000000 ) ) ;
#75876=ORIENTED_EDGE ( 'NONE', *, *, #123134, .F. ) ;
#75877=AXIS2_PLACEMENT_3D ( 'NONE', #94108, #117275, #84003 ) ;
#75878=ORIENTED_EDGE ( 'NONE', *, *, #94098, .T. ) ;
#75880=VERTEX_POINT ( 'NONE', #46791 ) ;
#75881=ORIENTED_EDGE ( 'NONE', *, *, #111550, .F. ) ;
#75883=ADVANCED_FACE ( 'NONE', ( #77944 ), #135202, .F. ) ;
#75884=CARTESIAN_POINT ( 'NONE',  ( 23.70025512860841133, -27.71228299555189523, 4.000000000000000000 ) ) ;
#75885=VERTEX_POINT ( 'NONE', #69213 ) ;
#75886=CARTESIAN_POINT ( 'NONE',  ( -18.51168605928420519, 6.759292476615645917, 16.35960578974473734 ) ) ;
#75887=CARTESIAN_POINT ( 'NONE',  ( 34.49999999999975131, -19.91253812416055879, 4.000000000000000000 ) ) ;
#75888=DIRECTION ( 'NONE',  ( 0.7071067811865487940, 0.7071067811865463515, -0.000000000000000000 ) ) ;
#75889=FACE_OUTER_BOUND ( 'NONE', #113461, .T. ) ;
#75890=CARTESIAN_POINT ( 'NONE',  ( -15.70710678118643422, 20.25929247661551713, 5.000000000000000000 ) ) ;
#75893=CARTESIAN_POINT ( 'NONE',  ( -60.48921356237309510, -27.52281430457097500, 5.000000000000000000 ) ) ;
#75894=DIRECTION ( 'NONE',  ( -0.000000000000000000, 1.000000000000000000, -0.000000000000000000 ) ) ;
#75895=ORIENTED_EDGE ( 'NONE', *, *, #118983, .F. ) ;
#75896=VERTEX_POINT ( 'NONE', #58380 ) ;
#75897=ORIENTED_EDGE ( 'NONE', *, *, #49074, .F. ) ;
#75899=ORIENTED_EDGE ( 'NONE', *, *, #20587, .T. ) ;
#75900=CARTESIAN_POINT ( 'NONE',  ( 12.18398860626900060, 28.73617430169795739, 5.000000000000000000 ) ) ;
#75901=EDGE_CURVE ( 'NONE', #92375, #39654, #35889, .T. ) ;
#75903=VECTOR ( 'NONE', #48978, 1000.000000000000000 ) ;
#75905=LINE ( 'NONE', #120077, #19374 ) ;
#75906=ADVANCED_FACE ( 'NONE', ( #12658 ), #68514, .T. ) ;
#75907=CARTESIAN_POINT ( 'NONE',  ( -39.29974487139159578, -27.71228299555233576, 4.000000000000000000 ) ) ;
#75908=VERTEX_POINT ( 'NONE', #1053 ) ;
#75909=LINE ( 'NONE', #20798, #2508 ) ;
#75910=CARTESIAN_POINT ( 'NONE',  ( 23.99999999999983302, -3.033600742197707145, 5.000000000000000000 ) ) ;
#75911=EDGE_CURVE ( 'NONE', #80946, #138457, #26734, .T. ) ;
#75912=EDGE_CURVE ( 'NONE', #112149, #99304, #45342, .T. ) ;
#75914=DIRECTION ( 'NONE',  ( -0.7071067811865487940, 0.7071067811865463515, -0.000000000000000000 ) ) ;
#75915=ORIENTED_EDGE ( 'NONE', *, *, #71343, .T. ) ;
#75917=DIRECTION ( 'NONE',  ( 0.7071067811865486830, -0.7071067811865464625, -0.000000000000000000 ) ) ;
#75918=ORIENTED_EDGE ( 'NONE', *, *, #33574, .T. ) ;
#75919=VERTEX_POINT ( 'NONE', #132353 ) ;
#75920=ORIENTED_EDGE ( 'NONE', *, *, #78909, .T. ) ;
#75922=ORIENTED_EDGE ( 'NONE', *, *, #112390, .T. ) ;
#75923=VECTOR ( 'NONE', #119231, 1000.000000000000227 ) ;
#75924=FACE_OUTER_BOUND ( 'NONE', #98583, .T. ) ;
#75926=EDGE_CURVE ( 'NONE', #109090, #1274, #121426, .T. ) ;
#75927=CARTESIAN_POINT ( 'NONE',  ( -39.48921356237310221, -27.52281430457082934, 5.000000000000000000 ) ) ;
#75929=ORIENTED_EDGE ( 'NONE', *, *, #132523, .F. ) ;
#75930=CARTESIAN_POINT ( 'NONE',  ( 0.000000000000000000, 0.000000000000000000, 5.000000000000000000 ) ) ;
#75932=EDGE_CURVE ( 'NONE', #24466, #8834, #110531, .T. ) ;
#75935=CARTESIAN_POINT ( 'NONE',  ( 19.49999999999987210, 18.05218569542898521, 5.000000000000000000 ) ) ;
#75936=CARTESIAN_POINT ( 'NONE',  ( 14.29289321881336328, -3.740707523384241728, 5.000000000000000000 ) ) ;
#75937=ORIENTED_EDGE ( 'NONE', *, *, #88675, .F. ) ;
#75938=ORIENTED_EDGE ( 'NONE', *, *, #103968, .F. ) ;
#75939=ORIENTED_EDGE ( 'NONE', *, *, #109675, .F. ) ;
#75943=LINE ( 'NONE', #9199, #95891 ) ;
#75944=DIRECTION ( 'NONE',  ( 0.7071067811865487940, -0.7071067811865463515, 0.000000000000000000 ) ) ;
#75945=CARTESIAN_POINT ( 'NONE',  ( 8.700255128608413102, -27.71228299555199825, 4.000000000000000000 ) ) ;
#75948=LINE ( 'NONE', #78102, #35164 ) ;
#75949=PLANE ( 'NONE',  #139218 ) ;
#75951=LINE ( 'NONE', #119422, #90305 ) ;
#75952=EDGE_CURVE ( 'NONE', #106121, #132680, #112006, .T. ) ;
#75953=ORIENTED_EDGE ( 'NONE', *, *, #13172, .F. ) ;
#75954=DIRECTION ( 'NONE',  ( 0.7071067811865487940, -0.7071067811865463515, 0.000000000000000000 ) ) ;
#75956=VECTOR ( 'NONE', #129241, 1000.000000000000114 ) ;
#75957=CARTESIAN_POINT ( 'NONE',  ( 16.82816939922341959, 9.759292476615618384, 4.000000000000000000 ) ) ;
#75958=DIRECTION ( 'NONE',  ( 0.7071067811865487940, -0.7071067811865463515, 0.000000000000000000 ) ) ;
#75960=DIRECTION ( 'NONE',  ( -0.3543493200069162685, -0.000000000000000000, -0.9351131265310288487 ) ) ;
#75961=EDGE_CURVE ( 'NONE', #4187, #28997, #90227, .T. ) ;
#75964=VECTOR ( 'NONE', #53045, 1000.000000000000000 ) ;
#75965=ORIENTED_EDGE ( 'NONE', *, *, #118737, .T. ) ;
#75966=PLANE ( 'NONE',  #90620 ) ;
#75967=ORIENTED_EDGE ( 'NONE', *, *, #41839, .T. ) ;
#75972=( BOUNDED_CURVE ( )  B_SPLINE_CURVE ( 3, ( #125014, #82256, #70676, #15502 ),
 .UNSPECIFIED., .F., .T. ) 
 B_SPLINE_CURVE_WITH_KNOTS ( ( 4, 4 ),
 ( 5.143245962375964986, 6.645403452391246191 ),
 .UNSPECIFIED. ) 
 CURVE ( )  GEOMETRIC_REPRESENTATION_ITEM ( )  RATIONAL_B_SPLINE_CURVE ( ( 1.000000000000000000, 0.8206354192515240564, 0.8206354192515240564, 1.000000000000000000 ) ) 
 REPRESENTATION_ITEM ( '' )  );
#75973=CARTESIAN_POINT ( 'NONE',  ( -8.999999999999952038, -22.22500000000000142, 4.412002311789987807 ) ) ;
#75976=LINE ( 'NONE', #120890, #20691 ) ;
#75981=CARTESIAN_POINT ( 'NONE',  ( -31.49999999999977973, 14.14708470758588099, -0.5283514160165838636 ) ) ;
#75982=VERTEX_POINT ( 'NONE', #6033 ) ;
#75984=VERTEX_POINT ( 'NONE', #61233 ) ;
#75985=DIRECTION ( 'NONE',  ( 1.000000000000000000, 0.000000000000000000, 0.000000000000000000 ) ) ;
#75986=ORIENTED_EDGE ( 'NONE', *, *, #72625, .F. ) ;
#75988=ADVANCED_FACE ( 'NONE', ( #127885 ), #16959, .F. ) ;
#75989=CARTESIAN_POINT ( 'NONE',  ( 5.510786437626906675, -27.52281430457051314, 5.000000000000000000 ) ) ;
#75990=LINE ( 'NONE', #20873, #143501 ) ;
#75993=DIRECTION ( 'NONE',  ( -0.000000000000000000, -0.000000000000000000, 1.000000000000000000 ) ) ;
#75994=CARTESIAN_POINT ( 'NONE',  ( -38.99451991528749062, 28.92564299267965211, 4.000000000000000000 ) ) ;
#75995=DIRECTION ( 'NONE',  ( 0.7071067811865487940, 0.7071067811865463515, 0.000000000000000000 ) ) ;
#75996=EDGE_CURVE ( 'NONE', #55245, #96439, #126416, .T. ) ;
#75998=DIRECTION ( 'NONE',  ( 0.7071067811865487940, 0.7071067811865463515, 0.000000000000000000 ) ) ;
#75999=ORIENTED_EDGE ( 'NONE', *, *, #131812, .F. ) ;
#76000=FACE_OUTER_BOUND ( 'NONE', #57069, .T. ) ;
#76003=DIRECTION ( 'NONE',  ( 0.7071067811865487940, 0.7071067811865463515, 0.000000000000000000 ) ) ;
#76004=CARTESIAN_POINT ( 'NONE',  ( 34.45011844616451668, -7.483719188362419672, 5.000000000000000888 ) ) ;
#76005=EDGE_LOOP ( 'NONE', ( #107298, #81669, #116827, #93895 ) ) ;
#76007=ORIENTED_EDGE ( 'NONE', *, *, #66793, .F. ) ;
#76010=ORIENTED_EDGE ( 'NONE', *, *, #1846, .F. ) ;
#76011=CARTESIAN_POINT ( 'NONE',  ( 15.48921356237309510, -27.52281430457066236, 5.000000000000000000 ) ) ;
#76012=ADVANCED_FACE ( 'NONE', ( #81535 ), #4580, .T. ) ;
#76013=FACE_OUTER_BOUND ( 'NONE', #88207, .T. ) ;
#76014=ORIENTED_EDGE ( 'NONE', *, *, #49898, .F. ) ;
#76015=DIRECTION ( 'NONE',  ( 0.7071067811865487940, 0.7071067811865463515, -0.000000000000000000 ) ) ;
#76016=CARTESIAN_POINT ( 'NONE',  ( 26.99999999999980815, 2.966399257802232459, 5.000000000000000000 ) ) ;
#76018=ORIENTED_EDGE ( 'NONE', *, *, #105693, .F. ) ;
#76019=VECTOR ( 'NONE', #137098, 1000.000000000000000 ) ;
#76020=EDGE_CURVE ( 'NONE', #88426, #128563, #28562, .T. ) ;
#76021=CARTESIAN_POINT ( 'NONE',  ( -68.99451991528748351, 28.92564299267986172, 4.000000000000000000 ) ) ;
#76022=DIRECTION ( 'NONE',  ( -0.7071067811865486830, -0.7071067811865464625, 0.000000000000000000 ) ) ;
#76024=VECTOR ( 'NONE', #74705, 1000.000000000000000 ) ;
#76026=ORIENTED_EDGE ( 'NONE', *, *, #34863, .F. ) ;
#76027=VECTOR ( 'NONE', #4658, 999.9999999999998863 ) ;
#76028=EDGE_CURVE ( 'NONE', #110799, #64904, #82241, .T. ) ;
#76029=VERTEX_POINT ( 'NONE', #27828 ) ;
#76030=LINE ( 'NONE', #42712, #141724 ) ;
#76032=EDGE_CURVE ( 'NONE', #79781, #3412, #93093, .T. ) ;
#76033=DIRECTION ( 'NONE',  ( 0.3543493200069162685, -0.000000000000000000, -0.9351131265310288487 ) ) ;
#76035=DIRECTION ( 'NONE',  ( -0.6830127018922181881, 0.6830127018922202975, -0.2588190451025214056 ) ) ;
#76036=VECTOR ( 'NONE', #115990, 1000.000000000000000 ) ;
#76037=AXIS2_PLACEMENT_3D ( 'NONE', #136862, #81808, #38273 ) ;
#76038=PLANE ( 'NONE',  #75729 ) ;
#76039=( BOUNDED_CURVE ( )  B_SPLINE_CURVE ( 3, ( #79074, #15172, #80480, #25350 ),
 .UNSPECIFIED., .F., .T. ) 
 B_SPLINE_CURVE_WITH_KNOTS ( ( 4, 4 ),
 ( 1.208578181583240374, 1.359146454359457135 ),
 .UNSPECIFIED. ) 
 CURVE ( )  GEOMETRIC_REPRESENTATION_ITEM ( )  RATIONAL_B_SPLINE_CURVE ( ( 1.000000000000000000, 0.9981116584018949744, 0.9981116584018949744, 1.000000000000000000 ) ) 
 REPRESENTATION_ITEM ( '' )  );
#76040=DIRECTION ( 'NONE',  ( 0.7071067811865487940, 0.7071067811865463515, 0.000000000000000000 ) ) ;
#76041=ORIENTED_EDGE ( 'NONE', *, *, #4508, .T. ) ;
#76044=PLANE ( 'NONE',  #3953 ) ;
#76045=VERTEX_POINT ( 'NONE', #105377 ) ;
#76046=ORIENTED_EDGE ( 'NONE', *, *, #61589, .F. ) ;
#76047=VECTOR ( 'NONE', #41518, 1000.000000000000227 ) ;
#76048=ADVANCED_FACE ( 'NONE', ( #6739 ), #116269, .F. ) ;
#76049=VECTOR ( 'NONE', #107157, 1000.000000000000227 ) ;
#76050=CARTESIAN_POINT ( 'NONE',  ( 15.06442625288295822, 7.619305877646135094, 4.652854425660932769 ) ) ;
#76051=ORIENTED_EDGE ( 'NONE', *, *, #42391, .F. ) ;
#76052=CARTESIAN_POINT ( 'NONE',  ( -4.171830600776445408, -8.240707523384198652, 4.000000000000000000 ) ) ;
#76054=DIRECTION ( 'NONE',  ( -0.000000000000000000, 0.3543493200069153248, 0.9351131265310292928 ) ) ;
#76055=CARTESIAN_POINT ( 'NONE',  ( 36.18398860626899705, 28.73617430169812437, 5.000000000000000000 ) ) ;
#76056=EDGE_CURVE ( 'NONE', #45188, #84616, #134902, .T. ) ;
#76057=CARTESIAN_POINT ( 'NONE',  ( 0.000000000000000000, 0.000000000000000000, 5.000000000000000000 ) ) ;
#76058=ORIENTED_EDGE ( 'NONE', *, *, #20812, .F. ) ;
#76059=AXIS2_PLACEMENT_3D ( 'NONE', #132317, #98239, #56902 ) ;
#76061=VECTOR ( 'NONE', #141327, 1000.000000000000000 ) ;
#76062=ORIENTED_EDGE ( 'NONE', *, *, #101240, .F. ) ;
#76063=FACE_OUTER_BOUND ( 'NONE', #985, .T. ) ;
#76064=EDGE_LOOP ( 'NONE', ( #41323, #93483, #116505, #123319 ) ) ;
#76065=DIRECTION ( 'NONE',  ( -0.7071067811865486830, -0.7071067811865464625, 0.000000000000000000 ) ) ;
#76066=ORIENTED_EDGE ( 'NONE', *, *, #3855, .T. ) ;
#76067=DIRECTION ( 'NONE',  ( 0.7071067811865487940, 0.7071067811865463515, -0.000000000000000000 ) ) ;
#76068=EDGE_LOOP ( 'NONE', ( #5763, #84818, #87095, #58660 ) ) ;
#76070=ORIENTED_EDGE ( 'NONE', *, *, #191, .F. ) ;
#76071=LINE ( 'NONE', #123162, #30407 ) ;
#76072=LINE ( 'NONE', #31853, #133195 ) ;
#76073=DIRECTION ( 'NONE',  ( 0.7071067811865487940, 0.7071067811865463515, 0.000000000000000000 ) ) ;
#76074=DIRECTION ( 'NONE',  ( 0.6830127018922181881, 0.6830127018922202975, -0.2588190451025214056 ) ) ;
#76076=DIRECTION ( 'NONE',  ( -0.7071067811865486830, 0.7071067811865464625, 0.000000000000000000 ) ) ;
#76077=EDGE_CURVE ( 'NONE', #139208, #82074, #83674, .T. ) ;
#76078=DIRECTION ( 'NONE',  ( 0.6830127018922181881, 0.6830127018922202975, -0.2588190451025214056 ) ) ;
#76079=DIRECTION ( 'NONE',  ( -0.3543493200069162685, -0.000000000000000000, -0.9351131265310288487 ) ) ;
#76080=AXIS2_PLACEMENT_3D ( 'NONE', #49750, #73619, #74344 ) ;
#76081=AXIS2_PLACEMENT_3D ( 'NONE', #126402, #17626, #61899 ) ;
#76082=ADVANCED_FACE ( 'NONE', ( #49624 ), #93799, .F. ) ;
#76083=EDGE_CURVE ( 'NONE', #141976, #56643, #113532, .T. ) ;
#76084=DIRECTION ( 'NONE',  ( -0.6830127018922181881, 0.6830127018922202975, -0.2588190451025214056 ) ) ;
#76085=PLANE ( 'NONE',  #13490 ) ;
#76086=DIRECTION ( 'NONE',  ( 0.6830127018922180770, -0.6830127018922204085, -0.2588190451025213501 ) ) ;
#76087=ORIENTED_EDGE ( 'NONE', *, *, #23147, .F. ) ;
#76088=ORIENTED_EDGE ( 'NONE', *, *, #21110, .T. ) ;
#76089=EDGE_LOOP ( 'NONE', ( #66004, #12255, #89620, #10419 ) ) ;
#76090=CARTESIAN_POINT ( 'NONE',  ( -27.48921356237309155, -27.52281430457074762, 5.000000000000000000 ) ) ;
#76091=ORIENTED_EDGE ( 'NONE', *, *, #47365, .T. ) ;
#76092=ADVANCED_FACE ( 'NONE', ( #36561 ), #80804, .F. ) ;
#76093=VERTEX_POINT ( 'NONE', #37287 ) ;
#76094=CARTESIAN_POINT ( 'NONE',  ( 0.000000000000000000, 0.000000000000000000, 5.000000000000000000 ) ) ;
#76096=EDGE_CURVE ( 'NONE', #20803, #19753, #38712, .T. ) ;
#76097=EDGE_CURVE ( 'NONE', #47758, #93680, #53897, .T. ) ;
#76098=CARTESIAN_POINT ( 'NONE',  ( 26.99999999999981171, -13.44781430457069149, 5.000000000000000000 ) ) ;
#76099=ORIENTED_EDGE ( 'NONE', *, *, #51157, .F. ) ;
#76100=LINE ( 'NONE', #99241, #132085 ) ;
#76101=ORIENTED_EDGE ( 'NONE', *, *, #13323, .T. ) ;
#76102=LINE ( 'NONE', #20988, #56170 ) ;
#76103=DIRECTION ( 'NONE',  ( -0.000000000000000000, -0.3543493200069152693, 0.9351131265310292928 ) ) ;
#76104=EDGE_CURVE ( 'NONE', #34254, #56788, #6102, .T. ) ;
#76106=ORIENTED_EDGE ( 'NONE', *, *, #4311, .F. ) ;
#76108=ADVANCED_FACE ( 'NONE', ( #119803 ), #119115, .F. ) ;
#76109=LINE ( 'NONE', #31887, #43623 ) ;
#76111=PLANE ( 'NONE',  #2496 ) ;
#76112=EDGE_LOOP ( 'NONE', ( #137082, #52109, #8465, #100442 ) ) ;
#76113=DIRECTION ( 'NONE',  ( -0.000000000000000000, 0.3543493200069153248, 0.9351131265310292928 ) ) ;
#76115=CARTESIAN_POINT ( 'NONE',  ( -62.99451991528749772, 28.92564299267982264, 4.000000000000000000 ) ) ;
#76116=VERTEX_POINT ( 'NONE', #42302 ) ;
#76117=CARTESIAN_POINT ( 'NONE',  ( -6.706123077391903387, 22.22500000000000142, 4.000000000000000000 ) ) ;
#76118=CARTESIAN_POINT ( 'NONE',  ( 34.92499999999998295, -1.199905483972814713, 4.759050581649325373 ) ) ;
#76119=EDGE_CURVE ( 'NONE', #111653, #37807, #20494, .T. ) ;
#76120=CARTESIAN_POINT ( 'NONE',  ( 34.49999999999976552, 18.05432934483075513, 4.994342998332162331 ) ) ;
#76121=CARTESIAN_POINT ( 'NONE',  ( 5.148183550381419948, 17.25929247661554200, 8.802941693769213316 ) ) ;
#76122=EDGE_LOOP ( 'NONE', ( #16439, #89385, #133672, #123197 ) ) ;
#76123=DIRECTION ( 'NONE',  ( 0.7071067811865487940, -0.7071067811865463515, 0.000000000000000000 ) ) ;
#76124=CARTESIAN_POINT ( 'NONE',  ( 10.82816939922345512, 3.759292476615674783, 4.000000000000000000 ) ) ;
#76125=DIRECTION ( 'NONE',  ( -0.6830127018922180770, -0.6830127018922204085, -0.2588190451025213501 ) ) ;
#76126=ORIENTED_EDGE ( 'NONE', *, *, #116159, .F. ) ;
#76129=VECTOR ( 'NONE', #130831, 1000.000000000000000 ) ;
#76130=VECTOR ( 'NONE', #56369, 1000.000000000000000 ) ;
#76132=CARTESIAN_POINT ( 'NONE',  ( -2.999999999999975131, -10.44781430457071991, 5.000000000000000000 ) ) ;
#76133=EDGE_LOOP ( 'NONE', ( #8585, #9846, #38463, #105079 ) ) ;
#76134=VECTOR ( 'NONE', #39885, 1000.000000000000000 ) ;
#76135=LINE ( 'NONE', #120301, #67224 ) ;
#76136=ORIENTED_EDGE ( 'NONE', *, *, #129750, .T. ) ;
#76138=CARTESIAN_POINT ( 'NONE',  ( -26.91685193227052864, 21.75929247661549581, 7.311836541447990001 ) ) ;
#76139=DIRECTION ( 'NONE',  ( 0.7071067811865487940, -0.7071067811865463515, 0.000000000000000000 ) ) ;
#76142=VERTEX_POINT ( 'NONE', #43006 ) ;
#76143=CARTESIAN_POINT ( 'NONE',  ( 45.18398860626900415, 28.73617430169818832, 5.000000000000000000 ) ) ;
#76145=LINE ( 'NONE', #52927, #45232 ) ;
#76146=ADVANCED_FACE ( 'NONE', ( #9619 ), #52424, .F. ) ;
#76147=LINE ( 'NONE', #109481, #104064 ) ;
#76149=CARTESIAN_POINT ( 'NONE',  ( -33.18398860626899705, 28.73617430169810305, 5.000000000000000000 ) ) ;
#76150=DIRECTION ( 'NONE',  ( 0.3543493200069162685, -0.000000000000000000, -0.9351131265310288487 ) ) ;
#76152=DIRECTION ( 'NONE',  ( 0.3543493200069162685, -0.000000000000000000, -0.9351131265310288487 ) ) ;
#76153=CARTESIAN_POINT ( 'NONE',  ( -34.92500000000001137, 22.22500000000000142, 4.500000000000000888 ) ) ;
#76154=DIRECTION ( 'NONE',  ( 0.7071067811865486830, -0.7071067811865464625, -0.000000000000000000 ) ) ;
#76155=VECTOR ( 'NONE', #19816, 1000.000000000000000 ) ;
#76156=ADVANCED_FACE ( 'NONE', ( #95936 ), #98091, .T. ) ;
#76161=ORIENTED_EDGE ( 'NONE', *, *, #98575, .T. ) ;
#76163=VECTOR ( 'NONE', #53325, 1000.000000000000000 ) ;
#76164=ORIENTED_EDGE ( 'NONE', *, *, #121954, .F. ) ;
#76165=VERTEX_POINT ( 'NONE', #40174 ) ;
#76166=ORIENTED_EDGE ( 'NONE', *, *, #7270, .F. ) ;
#76167=FACE_OUTER_BOUND ( 'NONE', #13726, .T. ) ;
#76168=VECTOR ( 'NONE', #82067, 1000.000000000000000 ) ;
#76169=CARTESIAN_POINT ( 'NONE',  ( 34.91764015037181679, 21.81495039010401982, 4.089230673112391301 ) ) ;
#76170=VERTEX_POINT ( 'NONE', #139491 ) ;
#76171=VECTOR ( 'NONE', #16420, 1000.000000000000000 ) ;
#76172=DIRECTION ( 'NONE',  ( -0.000000000000000000, -1.000000000000000000, -0.000000000000000000 ) ) ;
#76174=DIRECTION ( 'NONE',  ( 0.6830127018922181881, 0.6830127018922202975, -0.2588190451025214056 ) ) ;
#76177=DIRECTION ( 'NONE',  ( -0.6830127018922180770, -0.6830127018922204085, -0.2588190451025213501 ) ) ;
#76179=DIRECTION ( 'NONE',  ( 0.7071067811865487940, -0.7071067811865463515, 0.000000000000000000 ) ) ;
#76180=CARTESIAN_POINT ( 'NONE',  ( -21.15612307739224462, -22.22499999999999432, 4.000000000000000000 ) ) ;
#76181=CARTESIAN_POINT ( 'NONE',  ( 16.49999999999989697, 10.46639925780215918, 5.000000000000000000 ) ) ;
#76185=DIRECTION ( 'NONE',  ( 0.7071067811865486830, -0.7071067811865464625, -0.000000000000000000 ) ) ;
#76186=AXIS2_PLACEMENT_3D ( 'NONE', #115240, #139211, #128327 ) ;
#76189=ORIENTED_EDGE ( 'NONE', *, *, #89045, .F. ) ;
#76192=ORIENTED_EDGE ( 'NONE', *, *, #31380, .T. ) ;
#76194=FACE_OUTER_BOUND ( 'NONE', #134177, .T. ) ;
#76195=DIRECTION ( 'NONE',  ( -0.7071067811865486830, 0.7071067811865464625, 0.000000000000000000 ) ) ;
#76196=LINE ( 'NONE', #52284, #9870 ) ;
#76197=CARTESIAN_POINT ( 'NONE',  ( 11.99999999999992184, -1.068876922607797209, 4.000000000000000000 ) ) ;
#76199=VERTEX_POINT ( 'NONE', #108203 ) ;
#76200=EDGE_LOOP ( 'NONE', ( #54711, #28462, #80538, #2304 ) ) ;
#76201=DIRECTION ( 'NONE',  ( -0.7071067811865486830, -0.7071067811865464625, 0.000000000000000000 ) ) ;
#76202=CARTESIAN_POINT ( 'NONE',  ( 0.000000000000000000, 0.000000000000000000, 5.000000000000000000 ) ) ;
#76203=EDGE_CURVE ( 'NONE', #51263, #98176, #8863, .T. ) ;
#76204=CARTESIAN_POINT ( 'NONE',  ( 29.24139925780183091, 21.72500000000000853, 5.000000000000000000 ) ) ;
#76205=ORIENTED_EDGE ( 'NONE', *, *, #139798, .F. ) ;
#76207=ADVANCED_FACE ( 'NONE', ( #86512 ), #142325, .F. ) ;
#76208=ORIENTED_EDGE ( 'NONE', *, *, #2673, .F. ) ;
#76209=CARTESIAN_POINT ( 'NONE',  ( -11.99451991528749417, 28.92564299267946382, 4.000000000000000000 ) ) ;
#76210=LINE ( 'NONE', #53004, #113289 ) ;
#76211=CARTESIAN_POINT ( 'NONE',  ( 10.49999999999993250, -11.94781430457070392, 5.000000000000000000 ) ) ;
#76213=EDGE_CURVE ( 'NONE', #69257, #98086, #51744, .T. ) ;
#76214=ADVANCED_FACE ( 'NONE', ( #29954 ), #79238, .F. ) ;
#76216=ORIENTED_EDGE ( 'NONE', *, *, #136318, .T. ) ;
#76217=EDGE_CURVE ( 'NONE', #116804, #101800, #13187, .T. ) ;
#76218=DIRECTION ( 'NONE',  ( 0.7071067811865486830, -0.7071067811865464625, -0.000000000000000000 ) ) ;
#76219=ORIENTED_EDGE ( 'NONE', *, *, #29357, .F. ) ;
#76221=ORIENTED_EDGE ( 'NONE', *, *, #22610, .F. ) ;
#76222=EDGE_CURVE ( 'NONE', #26483, #56060, #24798, .T. ) ;
#76223=LINE ( 'NONE', #142212, #103063 ) ;
#76224=DIRECTION ( 'NONE',  ( -0.6830127018922181881, 0.6830127018922202975, -0.2588190451025214056 ) ) ;
#76226=ORIENTED_EDGE ( 'NONE', *, *, #111769, .F. ) ;
#76227=CARTESIAN_POINT ( 'NONE',  ( -34.49999999999976552, 6.054329344830883031, 4.994342998332166772 ) ) ;
#76228=CARTESIAN_POINT ( 'NONE',  ( -5.999999999999951150, -6.033600742197678279, 5.000000000000000000 ) ) ;
#76230=AXIS2_PLACEMENT_3D ( 'NONE', #53823, #130673, #97261 ) ;
#76231=EDGE_CURVE ( 'NONE', #54018, #136335, #78483, .T. ) ;
#76233=VECTOR ( 'NONE', #54810, 999.9999999999998863 ) ;
#76234=DIRECTION ( 'NONE',  ( 0.7071067811865487940, -0.7071067811865463515, 0.000000000000000000 ) ) ;
#76235=AXIS2_PLACEMENT_3D ( 'NONE', #118667, #7744, #107073 ) ;
#76236=FACE_BOUND ( 'NONE', #58282, .T. ) ;
#76237=ORIENTED_EDGE ( 'NONE', *, *, #119431, .F. ) ;
#76238=DIRECTION ( 'NONE',  ( 0.6830127018922181881, 0.6830127018922202975, -0.2588190451025214056 ) ) ;
#76239=CARTESIAN_POINT ( 'NONE',  ( -63.18398860626900415, 28.73617430169831621, 5.000000000000000000 ) ) ;
#76240=CARTESIAN_POINT ( 'NONE',  ( 26.20666063542134339, 21.75929247661549581, 4.998822639870700968 ) ) ;
#76241=ORIENTED_EDGE ( 'NONE', *, *, #124575, .F. ) ;
#76242=LINE ( 'NONE', #13090, #122170 ) ;
#76243=VERTEX_POINT ( 'NONE', #90800 ) ;
#76244=EDGE_CURVE ( 'NONE', #107481, #23113, #134297, .T. ) ;
#76245=ORIENTED_EDGE ( 'NONE', *, *, #121097, .F. ) ;
#76246=VECTOR ( 'NONE', #8680, 1000.000000000000000 ) ;
#76247=CARTESIAN_POINT ( 'NONE',  ( -32.99999999999977263, -13.97847968911263195, -0.1324546996127563547 ) ) ;
#76248=VERTEX_POINT ( 'NONE', #1588 ) ;
#76250=ORIENTED_EDGE ( 'NONE', *, *, #122522, .T. ) ;
#76251=PLANE ( 'NONE',  #20968 ) ;
#76252=DIRECTION ( 'NONE',  ( 0.7071067811865486830, -0.7071067811865464625, -0.000000000000000000 ) ) ;
#76253=EDGE_CURVE ( 'NONE', #22057, #45954, #121253, .T. ) ;
#76257=AXIS2_PLACEMENT_3D ( 'NONE', #78500, #53918, #44469 ) ;
#76260=ADVANCED_FACE ( 'NONE', ( #100234 ), #885, .F. ) ;
#76262=CARTESIAN_POINT ( 'NONE',  ( -34.92500000000002558, 18.66246187583879035, 4.000000000000000000 ) ) ;
#76263=DIRECTION ( 'NONE',  ( 0.3543493200069162685, -0.000000000000000000, -0.9351131265310288487 ) ) ;
#76264=DIRECTION ( 'NONE',  ( -0.7071067811865486830, 0.7071067811865464625, 0.000000000000000000 ) ) ;
#76265=DIRECTION ( 'NONE',  ( -0.7071067811865486830, 0.7071067811865464625, 0.000000000000000000 ) ) ;
#76266=VERTEX_POINT ( 'NONE', #89349 ) ;
#76267=VERTEX_POINT ( 'NONE', #57462 ) ;
#76268=ORIENTED_EDGE ( 'NONE', *, *, #75753, .F. ) ;
#76270=PLANE ( 'NONE',  #116775 ) ;
#76271=CARTESIAN_POINT ( 'NONE',  ( 75.29974487139158157, -27.71228299555258445, 4.000000000000000000 ) ) ;
#76274=EDGE_CURVE ( 'NONE', #102939, #15705, #66187, .T. ) ;
#76275=AXIS2_PLACEMENT_3D ( 'NONE', #75437, #34082, #76888 ) ;
#76276=ORIENTED_EDGE ( 'NONE', *, *, #68566, .T. ) ;
#76277=PLANE ( 'NONE',  #39745 ) ;
#76279=EDGE_CURVE ( 'NONE', #131061, #63704, #22623, .T. ) ;
#76280=VECTOR ( 'NONE', #23208, 1000.000000000000000 ) ;
#76282=VERTEX_POINT ( 'NONE', #56771 ) ;
#76283=VECTOR ( 'NONE', #80984, 1000.000000000000000 ) ;
#76284=CARTESIAN_POINT ( 'NONE',  ( -21.70701326429289324, -21.74070752338406010, 4.999753212805221558 ) ) ;
#76285=AXIS2_PLACEMENT_3D ( 'NONE', #110299, #34204, #100872 ) ;
#76288=DIRECTION ( 'NONE',  ( 0.7071067811865487940, 0.7071067811865463515, 0.000000000000000000 ) ) ;
#76289=ORIENTED_EDGE ( 'NONE', *, *, #6680, .F. ) ;
#76291=EDGE_CURVE ( 'NONE', #71113, #3366, #112528, .T. ) ;
#76292=DIRECTION ( 'NONE',  ( 0.3543493200069162685, -0.000000000000000000, -0.9351131265310288487 ) ) ;
#76293=FACE_OUTER_BOUND ( 'NONE', #34360, .T. ) ;
#76295=CARTESIAN_POINT ( 'NONE',  ( 30.18398860626900060, 28.73617430169808173, 5.000000000000000000 ) ) ;
#76298=ORIENTED_EDGE ( 'NONE', *, *, #37641, .T. ) ;
#76299=DIRECTION ( 'NONE',  ( 1.000000000000000000, 0.000000000000000000, 0.000000000000000000 ) ) ;
#76300=ADVANCED_FACE ( 'NONE', ( #66890 ), #32855, .F. ) ;
#76301=DIRECTION ( 'NONE',  ( -0.6830127018922180770, -0.6830127018922204085, -0.2588190451025213501 ) ) ;
#76302=DIRECTION ( 'NONE',  ( -0.000000000000000000, -0.3543493200069152693, 0.9351131265310292928 ) ) ;
#76303=EDGE_LOOP ( 'NONE', ( #34193, #86995, #2960, #102823 ) ) ;
#76304=DIRECTION ( 'NONE',  ( 0.6830127018922181881, 0.6830127018922202975, -0.2588190451025214056 ) ) ;
#76306=EDGE_LOOP ( 'NONE', ( #94329, #107635, #20226, #100605 ) ) ;
#76307=DIRECTION ( 'NONE',  ( -0.6830127018922181881, 0.6830127018922202975, -0.2588190451025214056 ) ) ;
#76310=CARTESIAN_POINT ( 'NONE',  ( 0.000000000000000000, -21.72500000000000142, 4.500000000000000888 ) ) ;
#76311=FACE_OUTER_BOUND ( 'NONE', #52795, .T. ) ;
#76312=ORIENTED_EDGE ( 'NONE', *, *, #45197, .T. ) ;
#76314=CARTESIAN_POINT ( 'NONE',  ( 20.90156419391750475, 11.25929247661559884, 10.79108189686412089 ) ) ;
#76315=PLANE ( 'NONE',  #78431 ) ;
#76317=LINE ( 'NONE', #120479, #48220 ) ;
#76318=EDGE_CURVE ( 'NONE', #38372, #133141, #10342, .T. ) ;
#76319=LINE ( 'NONE', #42986, #8914 ) ;
#76320=CARTESIAN_POINT ( 'NONE',  ( -25.49999999999982947, 10.94296225409024537, -9.576120664313316766 ) ) ;
#76322=FACE_OUTER_BOUND ( 'NONE', #234, .T. ) ;
#76323=CARTESIAN_POINT ( 'NONE',  ( 4.358242975411375397, 15.75929247661555799, 19.34181609438698857 ) ) ;
#76324=LINE ( 'NONE', #132867, #77189 ) ;
#76329=ORIENTED_EDGE ( 'NONE', *, *, #52801, .F. ) ;
#76330=LINE ( 'NONE', #57450, #55799 ) ;
#76331=VERTEX_POINT ( 'NONE', #11034 ) ;
#76333=DIRECTION ( 'NONE',  ( 0.7071067811865487940, 0.7071067811865463515, 0.000000000000000000 ) ) ;
#76335=AXIS2_PLACEMENT_3D ( 'NONE', #26871, #4337, #71121 ) ;
#76337=VECTOR ( 'NONE', #74146, 1000.000000000000000 ) ;
#76340=VECTOR ( 'NONE', #3133, 1000.000000000000000 ) ;
#76341=DIRECTION ( 'NONE',  ( 0.7071067811865486830, -0.7071067811865464625, -0.000000000000000000 ) ) ;
#76342=LINE ( 'NONE', #118392, #84720 ) ;
#76343=ORIENTED_EDGE ( 'NONE', *, *, #59902, .F. ) ;
#76344=CARTESIAN_POINT ( 'NONE',  ( -8.999999999999932498, 2.587461875839218273, 4.000000000000000000 ) ) ;
#76345=CARTESIAN_POINT ( 'NONE',  ( 60.18398860626900415, 28.73617430169829490, 5.000000000000000000 ) ) ;
#76346=CARTESIAN_POINT ( 'NONE',  ( -21.48921356237309155, -27.52281430457070499, 5.000000000000000000 ) ) ;
#76347=VECTOR ( 'NONE', #110871, 1000.000000000000000 ) ;
#76348=DIRECTION ( 'NONE',  ( -0.3543493200069162685, -0.000000000000000000, -0.9351131265310288487 ) ) ;
#76349=PLANE ( 'NONE',  #75217 ) ;
#76350=CARTESIAN_POINT ( 'NONE',  ( 31.49999999999977973, -19.91253812416055169, 4.000000000000000000 ) ) ;
#76351=DIRECTION ( 'NONE',  ( -0.6830127018922180770, -0.6830127018922204085, -0.2588190451025213501 ) ) ;
#76353=DIRECTION ( 'NONE',  ( -0.7071067811865486830, -0.7071067811865464625, 0.000000000000000000 ) ) ;
#76354=LINE ( 'NONE', #21248, #20666 ) ;
#76355=AXIS2_PLACEMENT_3D ( 'NONE', #138350, #58708, #60088 ) ;
#76356=ORIENTED_EDGE ( 'NONE', *, *, #2032, .T. ) ;
#76359=DIRECTION ( 'NONE',  ( -0.000000000000000000, 0.000000000000000000, 1.000000000000000000 ) ) ;
#76360=FACE_OUTER_BOUND ( 'NONE', #122311, .T. ) ;
#76362=DIRECTION ( 'NONE',  ( 0.7071067811865487940, 0.7071067811865463515, 0.000000000000000000 ) ) ;
#76363=EDGE_LOOP ( 'NONE', ( #124556, #54380, #119225, #110935 ) ) ;
#76365=DIRECTION ( 'NONE',  ( -0.000000000000000000, 0.000000000000000000, 1.000000000000000000 ) ) ;
#76368=VERTEX_POINT ( 'NONE', #124120 ) ;
#76370=ORIENTED_EDGE ( 'NONE', *, *, #62660, .F. ) ;
#76371=ORIENTED_EDGE ( 'NONE', *, *, #72231, .T. ) ;
#76372=LINE ( 'NONE', #66921, #72467 ) ;
#76373=VECTOR ( 'NONE', #67101, 1000.000000000000227 ) ;
#76374=VECTOR ( 'NONE', #126953, 999.9999999999998863 ) ;
#76375=FACE_OUTER_BOUND ( 'NONE', #34495, .T. ) ;
#76376=VECTOR ( 'NONE', #120885, 999.9999999999998863 ) ;
#76377=EDGE_CURVE ( 'NONE', #119974, #136740, #132889, .T. ) ;
#76378=LINE ( 'NONE', #7518, #78740 ) ;
#76379=ORIENTED_EDGE ( 'NONE', *, *, #49308, .F. ) ;
#76380=CARTESIAN_POINT ( 'NONE',  ( 0.000000000000000000, 0.000000000000000000, 5.000000000000000000 ) ) ;
#76381=DIRECTION ( 'NONE',  ( -0.7071067811865486830, -0.7071067811865464625, -0.000000000000000000 ) ) ;
#76382=ADVANCED_FACE ( 'NONE', ( #69047 ), #67636, .F. ) ;
#76384=FACE_OUTER_BOUND ( 'NONE', #99185, .T. ) ;
#76385=VERTEX_POINT ( 'NONE', #45872 ) ;
#76386=VECTOR ( 'NONE', #14314, 1000.000000000000000 ) ;
#76388=CARTESIAN_POINT ( 'NONE',  ( 69.48921356237309510, -27.52281430457103895, 5.000000000000000000 ) ) ;
#76390=DIRECTION ( 'NONE',  ( -0.000000000000000000, -0.3543493200069152693, 0.9351131265310292928 ) ) ;
#76391=VECTOR ( 'NONE', #108221, 1000.000000000000000 ) ;
#76392=CARTESIAN_POINT ( 'NONE',  ( -11.29298673570688649, -21.74070752338406720, 4.999753212805217117 ) ) ;
#76393=CARTESIAN_POINT ( 'NONE',  ( 29.99999999999978328, 11.58746187583914100, 4.000000000000000000 ) ) ;
#76394=ADVANCED_FACE ( 'NONE', ( #38546 ), #39270, .F. ) ;
#76395=ADVANCED_FACE ( 'NONE', ( #91507 ), #138576, .F. ) ;
#76396=ORIENTED_EDGE ( 'NONE', *, *, #143472, .F. ) ;
#76397=DIRECTION ( 'NONE',  ( -0.000000000000000000, 0.000000000000000000, 1.000000000000000000 ) ) ;
#76399=CARTESIAN_POINT ( 'NONE',  ( -21.70710678118639336, 14.25929247661557575, 5.000000000000000000 ) ) ;
#76401=DIRECTION ( 'NONE',  ( 0.7071067811865486830, -0.7071067811865464625, -0.000000000000000000 ) ) ;
#76403=VERTEX_POINT ( 'NONE', #37106 ) ;
#76404=VERTEX_POINT ( 'NONE', #135718 ) ;
#76405=VECTOR ( 'NONE', #2845, 999.9999999999998863 ) ;
#76406=EDGE_CURVE ( 'NONE', #63781, #140124, #81360, .T. ) ;
#76408=CARTESIAN_POINT ( 'NONE',  ( 17.57538274164440040, -2.608983483842240325, 5.000000000000000000 ) ) ;
#76410=ADVANCED_FACE ( 'NONE', ( #26245 ), #103088, .F. ) ;
#76411=ORIENTED_EDGE ( 'NONE', *, *, #48661, .F. ) ;
#76412=DIRECTION ( 'NONE',  ( -0.7071067811865487940, 0.7071067811865463515, 0.000000000000000000 ) ) ;
#76413=ORIENTED_EDGE ( 'NONE', *, *, #43027, .T. ) ;
#76414=LINE ( 'NONE', #77146, #5183 ) ;
#76415=PLANE ( 'NONE',  #126618 ) ;
#76416=VECTOR ( 'NONE', #5973, 999.9999999999998863 ) ;
#76418=LINE ( 'NONE', #77833, #125298 ) ;
#76419=FACE_BOUND ( 'NONE', #132549, .T. ) ;
#76421=CARTESIAN_POINT ( 'NONE',  ( 14.87852683662844022, -20.24070752338407431, 7.412974875817756271 ) ) ;
#76422=DIRECTION ( 'NONE',  ( 0.3543493200069162685, -0.000000000000000000, -0.9351131265310288487 ) ) ;
#76424=ORIENTED_EDGE ( 'NONE', *, *, #69830, .T. ) ;
#76425=EDGE_CURVE ( 'NONE', #75431, #53287, #70509, .T. ) ;
#76427=ORIENTED_EDGE ( 'NONE', *, *, #48773, .T. ) ;
#76428=ORIENTED_EDGE ( 'NONE', *, *, #126807, .T. ) ;
#76430=ORIENTED_EDGE ( 'NONE', *, *, #72997, .T. ) ;
#76431=LINE ( 'NONE', #62703, #105514 ) ;
#76432=CARTESIAN_POINT ( 'NONE',  ( 2.277185695429367662, -21.72499999999999432, 5.000000000000000000 ) ) ;
#76433=ADVANCED_FACE ( 'NONE', ( #36403 ), #83492, .T. ) ;
#76435=DIRECTION ( 'NONE',  ( 0.7071067811865486830, -0.7071067811865464625, -0.000000000000000000 ) ) ;
#76436=DIRECTION ( 'NONE',  ( -0.000000000000000000, 0.000000000000000000, 1.000000000000000000 ) ) ;
#76437=EDGE_CURVE ( 'NONE', #31525, #56636, #4406, .T. ) ;
#76438=CARTESIAN_POINT ( 'NONE',  ( -34.92500000000001137, -22.22500000000000142, 4.000000000000000000 ) ) ;
#76440=DIRECTION ( 'NONE',  ( -0.7071067811865487940, 0.7071067811865463515, -0.000000000000000000 ) ) ;
#76443=CARTESIAN_POINT ( 'NONE',  ( -15.70612307739185276, 22.22500000000000142, 4.000000000000000000 ) ) ;
#76444=DIRECTION ( 'NONE',  ( -0.7071067811865487940, 0.7071067811865463515, -0.000000000000000000 ) ) ;
#76445=VECTOR ( 'NONE', #66936, 1000.000000000000000 ) ;
#76446=EDGE_LOOP ( 'NONE', ( #7293, #71102, #118270, #96210 ) ) ;
#76447=VECTOR ( 'NONE', #46543, 1000.000000000000000 ) ;
#76448=VECTOR ( 'NONE', #111615, 1000.000000000000000 ) ;
#76452=ADVANCED_FACE ( 'NONE', ( #71918 ), #5875, .F. ) ;
#76453=LINE ( 'NONE', #34359, #86038 ) ;
#76454=EDGE_CURVE ( 'NONE', #124853, #103174, #90590, .T. ) ;
#76456=VERTEX_POINT ( 'NONE', #61064 ) ;
#76457=VERTEX_POINT ( 'NONE', #82085 ) ;
#76459=VERTEX_POINT ( 'NONE', #80632 ) ;
#76462=EDGE_CURVE ( 'NONE', #13854, #19029, #113955, .T. ) ;
#76467=EDGE_CURVE ( 'NONE', #33777, #92406, #26941, .T. ) ;
#76468=CARTESIAN_POINT ( 'NONE',  ( 33.18398860626899705, 28.73617430169810305, 5.000000000000000000 ) ) ;
#76469=VERTEX_POINT ( 'NONE', #13903 ) ;
#76470=CARTESIAN_POINT ( 'NONE',  ( 11.99999999999991296, 16.93112307739200872, 4.000000000000000000 ) ) ;
#76471=AXIS2_PLACEMENT_3D ( 'NONE', #68881, #45706, #33413 ) ;
#76472=DIRECTION ( 'NONE',  ( -1.000000000000000000, 0.000000000000000000, 0.000000000000000000 ) ) ;
#76473=PLANE ( 'NONE',  #142072 ) ;
#76476=CARTESIAN_POINT ( 'NONE',  ( -33.79289321881321939, 3.759292476615681888, 5.000000000000000000 ) ) ;
#76477=CARTESIAN_POINT ( 'NONE',  ( 6.183988606268994381, 28.73617430169791476, 5.000000000000000000 ) ) ;
#76478=FACE_OUTER_BOUND ( 'NONE', #129460, .T. ) ;
#76479=ORIENTED_EDGE ( 'NONE', *, *, #99468, .F. ) ;
#76480=VECTOR ( 'NONE', #54629, 999.9999999999998863 ) ;
#76481=DIRECTION ( 'NONE',  ( -0.6830127018922181881, 0.6830127018922202975, -0.2588190451025214056 ) ) ;
#76482=ORIENTED_EDGE ( 'NONE', *, *, #26386, .F. ) ;
#76483=ORIENTED_EDGE ( 'NONE', *, *, #140049, .F. ) ;
#76484=VERTEX_POINT ( 'NONE', #71191 ) ;
#76485=AXIS2_PLACEMENT_3D ( 'NONE', #68518, #38020, #112701 ) ;
#76486=CARTESIAN_POINT ( 'NONE',  ( -8.510786437626906675, -27.52281430457049183, 5.000000000000000000 ) ) ;
#76487=PLANE ( 'NONE',  #34851 ) ;
#76488=CARTESIAN_POINT ( 'NONE',  ( 30.48921356237309510, -27.52281430457076894, 5.000000000000000000 ) ) ;
#76489=VECTOR ( 'NONE', #35557, 1000.000000000000000 ) ;
#76491=LINE ( 'NONE', #19928, #109561 ) ;
#76492=EDGE_CURVE ( 'NONE', #93995, #73867, #115339, .T. ) ;
#76494=ORIENTED_EDGE ( 'NONE', *, *, #19635, .F. ) ;
#76495=AXIS2_PLACEMENT_3D ( 'NONE', #108520, #21561, #133201 ) ;
#76497=ORIENTED_EDGE ( 'NONE', *, *, #107634, .T. ) ;
#76499=CARTESIAN_POINT ( 'NONE',  ( -63.48921356237309510, -27.52281430457099631, 5.000000000000000000 ) ) ;
#76500=LINE ( 'NONE', #19937, #64688 ) ;
#76502=VECTOR ( 'NONE', #19870, 1000.000000000000000 ) ;
#76503=DIRECTION ( 'NONE',  ( 1.000000000000000000, 0.000000000000000000, 0.000000000000000000 ) ) ;
#76504=LINE ( 'NONE', #128885, #62684 ) ;
#76505=PLANE ( 'NONE',  #46772 ) ;
#76506=VERTEX_POINT ( 'NONE', #84897 ) ;
#76507=ORIENTED_EDGE ( 'NONE', *, *, #44170, .F. ) ;
#76509=AXIS2_PLACEMENT_3D ( 'NONE', #65491, #54595, #100233 ) ;
#76510=FACE_OUTER_BOUND ( 'NONE', #32661, .T. ) ;
#76512=DIRECTION ( 'NONE',  ( 0.7071067811865486830, -0.7071067811865464625, -0.000000000000000000 ) ) ;
#76514=ADVANCED_FACE ( 'NONE', ( #116808 ), #86345, .F. ) ;
#76517=EDGE_CURVE ( 'NONE', #89322, #99498, #142161, .T. ) ;
#76518=LINE ( 'NONE', #141772, #95092 ) ;
#76519=CARTESIAN_POINT ( 'NONE',  ( -39.29974487139159578, -27.71228299555233576, 4.000000000000000000 ) ) ;
#76520=ORIENTED_EDGE ( 'NONE', *, *, #73788, .F. ) ;
#76521=CARTESIAN_POINT ( 'NONE',  ( -27.29974487139158512, -27.71228299555225405, 4.000000000000000000 ) ) ;
#76522=EDGE_LOOP ( 'NONE', ( #40045, #131116, #9745, #16556 ) ) ;
#76524=DIRECTION ( 'NONE',  ( -0.7071067811865486830, -0.7071067811865464625, 0.000000000000000000 ) ) ;
#76526=DIRECTION ( 'NONE',  ( -0.000000000000000000, 0.000000000000000000, 1.000000000000000000 ) ) ;
#76527=CARTESIAN_POINT ( 'NONE',  ( -36.29974487139159578, -27.71228299555231445, 4.000000000000000000 ) ) ;
#76528=CARTESIAN_POINT ( 'NONE',  ( 8.999999999999932498, 19.93112307739198386, 4.000000000000000000 ) ) ;
#76529=EDGE_CURVE ( 'NONE', #124509, #142351, #41386, .T. ) ;
#76531=PLANE ( 'NONE',  #38002 ) ;
#76532=ORIENTED_EDGE ( 'NONE', *, *, #54761, .T. ) ;
#76533=ORIENTED_EDGE ( 'NONE', *, *, #28548, .T. ) ;
#76534=DIRECTION ( 'NONE',  ( 0.7071067811865486830, -0.7071067811865464625, -0.000000000000000000 ) ) ;
#76537=AXIS2_PLACEMENT_3D ( 'NONE', #3207, #24954, #133748 ) ;
#76538=CARTESIAN_POINT ( 'NONE',  ( -11.99999999999992184, 13.93112307739204603, 4.000000000000000000 ) ) ;
#76541=DIRECTION ( 'NONE',  ( 0.6830127018922181881, 0.6830127018922202975, -0.2588190451025214056 ) ) ;
#76542=CARTESIAN_POINT ( 'NONE',  ( 34.92499999999998295, -10.19990548397272256, 4.759050581649326261 ) ) ;
#76543=ORIENTED_EDGE ( 'NONE', *, *, #23950, .T. ) ;
#76545=CARTESIAN_POINT ( 'NONE',  ( 21.29974487139158512, -27.71228299555221142, 4.000000000000000000 ) ) ;
#76546=DIRECTION ( 'NONE',  ( 0.7071067811865486830, -0.7071067811865464625, -0.000000000000000000 ) ) ;
#76547=CARTESIAN_POINT ( 'NONE',  ( -10.49999999999992184, 19.39370406404966118, 1.459788787078225569 ) ) ;
#76548=EDGE_LOOP ( 'NONE', ( #112726, #105926, #10747, #21469 ) ) ;
#76552=VECTOR ( 'NONE', #83725, 1000.000000000000000 ) ;
#76554=EDGE_LOOP ( 'NONE', ( #139344, #2523, #137443, #83567 ) ) ;
#76556=VECTOR ( 'NONE', #23863, 999.9999999999998863 ) ;
#76557=AXIS2_PLACEMENT_3D ( 'NONE', #119428, #130353, #97704 ) ;
#76558=VECTOR ( 'NONE', #82538, 1000.000000000000000 ) ;
#76559=AXIS2_PLACEMENT_3D ( 'NONE', #116836, #17512, #74051 ) ;
#76560=CARTESIAN_POINT ( 'NONE',  ( -39.18398860626899705, 28.73617430169814568, 5.000000000000000000 ) ) ;
#76561=AXIS2_PLACEMENT_3D ( 'NONE', #24377, #36668, #68625 ) ;
#76562=CARTESIAN_POINT ( 'NONE',  ( -36.18398860626899705, 28.73617430169812437, 5.000000000000000000 ) ) ;
#76563=DIRECTION ( 'NONE',  ( -0.000000000000000000, -0.3543493200069152693, 0.9351131265310292928 ) ) ;
#76564=LINE ( 'NONE', #77290, #57870 ) ;
#76566=EDGE_CURVE ( 'NONE', #79108, #60521, #130564, .T. ) ;
#76567=CARTESIAN_POINT ( 'NONE',  ( -42.48921356237308800, -27.52281430457085065, 5.000000000000000000 ) ) ;
#76568=ORIENTED_EDGE ( 'NONE', *, *, #21118, .T. ) ;
#76569=LINE ( 'NONE', #66397, #46181 ) ;
#76570=DIRECTION ( 'NONE',  ( 1.000000000000000000, 0.000000000000000000, 0.000000000000000000 ) ) ;
#76571=CARTESIAN_POINT ( 'NONE',  ( 2.999999999999993783, 2.587461875839212944, 4.000000000000000000 ) ) ;
#76572=VECTOR ( 'NONE', #134865, 1000.000000000000000 ) ;
#76573=CARTESIAN_POINT ( 'NONE',  ( 17.81601139373099940, 28.73617430169775133, 5.000000000000000000 ) ) ;
#76574=ORIENTED_EDGE ( 'NONE', *, *, #36798, .T. ) ;
#76575=EDGE_CURVE ( 'NONE', #65577, #68093, #84221, .T. ) ;
#76576=VERTEX_POINT ( 'NONE', #40692 ) ;
#76577=EDGE_CURVE ( 'NONE', #120738, #53245, #118215, .T. ) ;
#76579=VERTEX_POINT ( 'NONE', #119635 ) ;
#76580=EDGE_CURVE ( 'NONE', #58068, #34917, #74030, .T. ) ;
#76581=FACE_OUTER_BOUND ( 'NONE', #43403, .T. ) ;
#76582=CARTESIAN_POINT ( 'NONE',  ( -34.49999999999976552, 0.05432934483094037370, 4.994342998332168548 ) ) ;
#76584=AXIS2_PLACEMENT_3D ( 'NONE', #55637, #3358, #66514 ) ;
#76587=ORIENTED_EDGE ( 'NONE', *, *, #132431, .T. ) ;
#76588=ADVANCED_FACE ( 'NONE', ( #20332 ), #64576, .F. ) ;
#76589=PLANE ( 'NONE',  #23694 ) ;
#76591=VECTOR ( 'NONE', #129339, 999.9999999999998863 ) ;
#76593=VERTEX_POINT ( 'NONE', #95769 ) ;
#76594=AXIS2_PLACEMENT_3D ( 'NONE', #48796, #137229, #37930 ) ;
#76595=CARTESIAN_POINT ( 'NONE',  ( -18.38945826904184599, 9.109118024354394549, 4.348864708961791337 ) ) ;
#76596=VECTOR ( 'NONE', #104503, 1000.000000000000000 ) ;
#76598=FACE_OUTER_BOUND ( 'NONE', #130623, .T. ) ;
#76599=VECTOR ( 'NONE', #129430, 1000.000000000000227 ) ;
#76600=EDGE_LOOP ( 'NONE', ( #130647, #141798, #65425, #10917 ) ) ;
#76601=EDGE_CURVE ( 'NONE', #110589, #125118, #6572, .T. ) ;
#76602=ADVANCED_FACE ( 'NONE', ( #50848 ), #139316, .T. ) ;
#76603=FACE_BOUND ( 'NONE', #43462, .T. ) ;
#76606=DIRECTION ( 'NONE',  ( -0.7071067811865487940, 0.7071067811865463515, -0.000000000000000000 ) ) ;
#76608=DIRECTION ( 'NONE',  ( -0.7071067811865486830, -0.7071067811865464625, -0.000000000000000000 ) ) ;
#76609=EDGE_CURVE ( 'NONE', #32796, #10266, #108754, .T. ) ;
#76611=EDGE_LOOP ( 'NONE', ( #111291, #26798, #75479, #88350 ) ) ;
#76612=AXIS2_PLACEMENT_3D ( 'NONE', #10501, #143174, #21406 ) ;
#76613=EDGE_LOOP ( 'NONE', ( #118341, #142337, #26519, #81753 ) ) ;
#76617=VECTOR ( 'NONE', #61743, 1000.000000000000227 ) ;
#76619=DIRECTION ( 'NONE',  ( 0.7071067811865487940, -0.7071067811865463515, 0.000000000000000000 ) ) ;
#76620=DIRECTION ( 'NONE',  ( 0.6830127018922180770, -0.6830127018922204085, -0.2588190451025213501 ) ) ;
#76621=ORIENTED_EDGE ( 'NONE', *, *, #101411, .T. ) ;
#76622=DIRECTION ( 'NONE',  ( -0.6830127018922180770, -0.6830127018922204085, -0.2588190451025213501 ) ) ;
#76623=CARTESIAN_POINT ( 'NONE',  ( 12.48921356237309155, -27.52281430457064104, 5.000000000000000000 ) ) ;
#76624=CARTESIAN_POINT ( 'NONE',  ( 34.92499999999998295, 17.81665438641027777, 4.500000000000000888 ) ) ;
#76625=DIRECTION ( 'NONE',  ( -0.7071067811865487940, 0.7071067811865463515, 0.000000000000000000 ) ) ;
#76626=ADVANCED_FACE ( 'NONE', ( #97924 ), #63188, .F. ) ;
#76627=LINE ( 'NONE', #9141, #127227 ) ;
#76628=VECTOR ( 'NONE', #36690, 1000.000000000000000 ) ;
#76630=VERTEX_POINT ( 'NONE', #140692 ) ;
#76631=CARTESIAN_POINT ( 'NONE',  ( 20.99451991528748707, 28.92564299267952777, 4.000000000000000000 ) ) ;
#76632=LINE ( 'NONE', #122967, #90495 ) ;
#76633=VERTEX_POINT ( 'NONE', #101478 ) ;
#76634=ORIENTED_EDGE ( 'NONE', *, *, #53845, .T. ) ;
#76635=EDGE_LOOP ( 'NONE', ( #86396, #27454, #104780, #111844 ) ) ;
#76638=AXIS2_PLACEMENT_3D ( 'NONE', #44221, #100013, #111593 ) ;
#76639=EDGE_CURVE ( 'NONE', #15951, #44387, #33418, .T. ) ;
#76640=DIRECTION ( 'NONE',  ( 0.7071067811865487940, -0.7071067811865463515, 0.000000000000000000 ) ) ;
#76643=CARTESIAN_POINT ( 'NONE',  ( 31.00193056682077142, -22.22500000000000142, 4.500000000000000888 ) ) ;
#76645=ORIENTED_EDGE ( 'NONE', *, *, #135614, .T. ) ;
#76646=CARTESIAN_POINT ( 'NONE',  ( 42.29974487139158157, -27.71228299555235708, 4.000000000000000000 ) ) ;
#76647=AXIS2_PLACEMENT_3D ( 'NONE', #113000, #2811, #56552 ) ;
#76648=DIRECTION ( 'NONE',  ( 1.000000000000000000, 0.000000000000000000, 0.000000000000000000 ) ) ;
#76649=LINE ( 'NONE', #9927, #23631 ) ;
#76650=VECTOR ( 'NONE', #135976, 1000.000000000000227 ) ;
#76652=VECTOR ( 'NONE', #120205, 1000.000000000000000 ) ;
#76653=EDGE_LOOP ( 'NONE', ( #73252, #62236, #36143, #115203 ) ) ;
#76655=EDGE_CURVE ( 'NONE', #19199, #98173, #66034, .T. ) ;
#76656=VERTEX_POINT ( 'NONE', #10871 ) ;
#76657=VERTEX_POINT ( 'NONE', #2128 ) ;
#76660=AXIS2_PLACEMENT_3D ( 'NONE', #24264, #56922, #1745 ) ;
#76661=EDGE_LOOP ( 'NONE', ( #57186, #77442, #35632, #48728 ) ) ;
#76662=VECTOR ( 'NONE', #12641, 1000.000000000000000 ) ;
#76663=VECTOR ( 'NONE', #128445, 999.9999999999998863 ) ;
#76664=AXIS2_PLACEMENT_3D ( 'NONE', #130685, #121195, #32799 ) ;
#76666=ADVANCED_FACE ( 'NONE', ( #65324 ), #721, .F. ) ;
#76667=LINE ( 'NONE', #22227, #138945 ) ;
#76668=ORIENTED_EDGE ( 'NONE', *, *, #89746, .T. ) ;
#76669=CARTESIAN_POINT ( 'NONE',  ( -5.277185695429377432, -21.72500000000000853, 5.000000000000000000 ) ) ;
#76670=VECTOR ( 'NONE', #58585, 1000.000000000000000 ) ;
#76671=VERTEX_POINT ( 'NONE', #55869 ) ;
#76673=EDGE_CURVE ( 'NONE', #13309, #32684, #121788, .T. ) ;
#76674=CARTESIAN_POINT ( 'NONE',  ( -8.994519915287490619, 28.92564299267944250, 4.000000000000000000 ) ) ;
#76675=VECTOR ( 'NONE', #59842, 1000.000000000000000 ) ;
#76677=ORIENTED_EDGE ( 'NONE', *, *, #28506, .T. ) ;
#76678=ORIENTED_EDGE ( 'NONE', *, *, #57926, .T. ) ;
#76680=AXIS2_PLACEMENT_3D ( 'NONE', #29762, #139999, #7288 ) ;
#76683=LINE ( 'NONE', #120857, #68220 ) ;
#76684=FACE_OUTER_BOUND ( 'NONE', #38465, .T. ) ;
#76685=VECTOR ( 'NONE', #74091, 999.9999999999998863 ) ;
#76686=AXIS2_PLACEMENT_3D ( 'NONE', #3920, #2513, #133094 ) ;
#76687=LINE ( 'NONE', #85375, #143313 ) ;
#76688=ADVANCED_FACE ( 'NONE', ( #66723 ), #44278, .F. ) ;
#76690=PLANE ( 'NONE',  #134720 ) ;
#76693=ORIENTED_EDGE ( 'NONE', *, *, #24659, .F. ) ;
#76694=LINE ( 'NONE', #97696, #83393 ) ;
#76695=VERTEX_POINT ( 'NONE', #90628 ) ;
#76697=VECTOR ( 'NONE', #24781, 1000.000000000000227 ) ;
#76698=ORIENTED_EDGE ( 'NONE', *, *, #63054, .T. ) ;
#76699=PLANE ( 'NONE',  #20568 ) ;
#76700=DIRECTION ( 'NONE',  ( -0.7071067811865486830, -0.7071067811865464625, 0.000000000000000000 ) ) ;
#76702=VECTOR ( 'NONE', #57277, 1000.000000000000227 ) ;
#76703=EDGE_CURVE ( 'NONE', #54005, #109319, #31950, .T. ) ;
#76704=CARTESIAN_POINT ( 'NONE',  ( 15.79289321881335084, 9.759292476615625489, 5.000000000000000000 ) ) ;
#76705=VERTEX_POINT ( 'NONE', #34107 ) ;
#76707=EDGE_LOOP ( 'NONE', ( #5423, #67325, #6292, #9241 ) ) ;
#76708=CARTESIAN_POINT ( 'NONE',  ( -66.48921356237309510, -27.52281430457101763, 5.000000000000000000 ) ) ;
#76712=CARTESIAN_POINT ( 'NONE',  ( 6.707013264292989163, -21.74070752338407075, 4.999753212805213565 ) ) ;
#76715=AXIS2_PLACEMENT_3D ( 'NONE', #88178, #33120, #33805 ) ;
#76717=FACE_OUTER_BOUND ( 'NONE', #92090, .T. ) ;
#76718=DIRECTION ( 'NONE',  ( -0.000000000000000000, -0.3543493200069152693, 0.9351131265310292928 ) ) ;
#76719=DIRECTION ( 'NONE',  ( 0.7071067811865486830, -0.7071067811865464625, -0.000000000000000000 ) ) ;
#76722=CARTESIAN_POINT ( 'NONE',  ( -7.828169399223476432, -8.240707523384205757, 4.000000000000000000 ) ) ;
#76723=AXIS2_PLACEMENT_3D ( 'NONE', #126733, #27422, #86835 ) ;
#76724=DIRECTION ( 'NONE',  ( -0.6830127018922181881, 0.6830127018922202975, -0.2588190451025214056 ) ) ;
#76725=ORIENTED_EDGE ( 'NONE', *, *, #114829, .F. ) ;
#76727=LINE ( 'NONE', #120154, #99916 ) ;
#76728=ORIENTED_EDGE ( 'NONE', *, *, #137422, .T. ) ;
#76729=LINE ( 'NONE', #46244, #131352 ) ;
#76731=VECTOR ( 'NONE', #63838, 1000.000000000000000 ) ;
#76732=CARTESIAN_POINT ( 'NONE',  ( -22.49999999999983302, 22.08746187583901843, 4.000000000000000000 ) ) ;
#76733=EDGE_LOOP ( 'NONE', ( #125388, #117860, #74449, #120215 ) ) ;
#76734=DIRECTION ( 'NONE',  ( -0.7071067811865486830, -0.7071067811865464625, 0.000000000000000000 ) ) ;
#76735=( BOUNDED_CURVE ( )  B_SPLINE_CURVE ( 3, ( #117134, #59936, #139658, #4763 ),
 .UNSPECIFIED., .F., .F. ) 
 B_SPLINE_CURVE_WITH_KNOTS ( ( 4, 4 ),
 ( 5.143245962375964986, 6.645403452391247079 ),
 .UNSPECIFIED. ) 
 CURVE ( )  GEOMETRIC_REPRESENTATION_ITEM ( )  RATIONAL_B_SPLINE_CURVE ( ( 1.000000000000000000, 0.8206354192515239454, 0.8206354192515239454, 1.000000000000000000 ) ) 
 REPRESENTATION_ITEM ( '' )  );
#76736=PLANE ( 'NONE',  #69644 ) ;
#76737=FACE_OUTER_BOUND ( 'NONE', #117781, .T. ) ;
#76740=ORIENTED_EDGE ( 'NONE', *, *, #127452, .T. ) ;
#76741=PLANE ( 'NONE',  #88303 ) ;
#76742=AXIS2_PLACEMENT_3D ( 'NONE', #1427, #100071, #12325 ) ;
#76745=DIRECTION ( 'NONE',  ( -0.000000000000000000, 0.000000000000000000, 1.000000000000000000 ) ) ;
#76746=EDGE_LOOP ( 'NONE', ( #9763, #114852, #96999, #27024 ) ) ;
#76747=VERTEX_POINT ( 'NONE', #54445 ) ;
#76749=EDGE_CURVE ( 'NONE', #123646, #17485, #110199, .T. ) ;
#76754=EDGE_CURVE ( 'NONE', #18784, #97146, #98619, .T. ) ;
#76756=ORIENTED_EDGE ( 'NONE', *, *, #73313, .T. ) ;
#76757=VECTOR ( 'NONE', #108346, 1000.000000000000000 ) ;
#76758=ADVANCED_FACE ( 'NONE', ( #131991 ), #45016, .F. ) ;
#76759=PLANE ( 'NONE',  #99972 ) ;
#76760=LINE ( 'NONE', #74608, #58271 ) ;
#76761=AXIS2_PLACEMENT_3D ( 'NONE', #3812, #136507, #92281 ) ;
#76762=VECTOR ( 'NONE', #88729, 1000.000000000000000 ) ;
#76764=EDGE_LOOP ( 'NONE', ( #35624, #107405, #44537, #42252 ) ) ;
#76765=DIRECTION ( 'NONE',  ( -0.000000000000000000, -0.3543493200069152693, 0.9351131265310292928 ) ) ;
#76766=VECTOR ( 'NONE', #33374, 1000.000000000000000 ) ;
#76767=CIRCLE ( 'NONE', #51291, 5.968999999999998529 ) ;
#76768=CARTESIAN_POINT ( 'NONE',  ( -34.92500000000001137, 11.71849043720411032, 4.759050581649336920 ) ) ;
#76769=VECTOR ( 'NONE', #75272, 999.9999999999998863 ) ;
#76770=VECTOR ( 'NONE', #139872, 1000.000000000000000 ) ;
#76773=ADVANCED_FACE ( 'NONE', ( #84215 ), #88488, .F. ) ;
#76774=ORIENTED_EDGE ( 'NONE', *, *, #116942, .F. ) ;
#76775=LINE ( 'NONE', #107905, #37618 ) ;
#76776=ADVANCED_FACE ( 'NONE', ( #134130 ), #89194, .F. ) ;
#76777=PLANE ( 'NONE',  #31628 ) ;
#76779=DIRECTION ( 'NONE',  ( 0.7071067811865486830, -0.7071067811865464625, -0.000000000000000000 ) ) ;
#76780=AXIS2_PLACEMENT_3D ( 'NONE', #32148, #29991, #97370 ) ;
#76782=EDGE_CURVE ( 'NONE', #95164, #123516, #56609, .T. ) ;
#76783=FACE_OUTER_BOUND ( 'NONE', #37775, .T. ) ;
#76784=EDGE_LOOP ( 'NONE', ( #95582, #111013, #20127, #121938 ) ) ;
#76785=EDGE_LOOP ( 'NONE', ( #24383, #96371, #103355, #119919 ) ) ;
#76786=VECTOR ( 'NONE', #21324, 1000.000000000000000 ) ;
#76787=DIRECTION ( 'NONE',  ( -0.7071067811865486830, -0.7071067811865464625, 0.000000000000000000 ) ) ;
#76788=ORIENTED_EDGE ( 'NONE', *, *, #110926, .F. ) ;
#76792=VECTOR ( 'NONE', #39679, 1000.000000000000000 ) ;
#76793=LINE ( 'NONE', #130444, #65950 ) ;
#76794=ORIENTED_EDGE ( 'NONE', *, *, #83811, .T. ) ;
#76797=VECTOR ( 'NONE', #67560, 1000.000000000000000 ) ;
#76798=CARTESIAN_POINT ( 'NONE',  ( 1.045157733366657071, -21.74070752338406010, 21.72585301388584611 ) ) ;
#76800=CARTESIAN_POINT ( 'NONE',  ( -8.999999999999925393, -19.44781430457063465, 5.000000000000000000 ) ) ;
#76801=VECTOR ( 'NONE', #49961, 1000.000000000000000 ) ;
#76803=ORIENTED_EDGE ( 'NONE', *, *, #65433, .T. ) ;
#76804=DIRECTION ( 'NONE',  ( -0.7071067811865487940, 0.7071067811865463515, -0.000000000000000000 ) ) ;
#76805=ORIENTED_EDGE ( 'NONE', *, *, #77919, .T. ) ;
#76806=CARTESIAN_POINT ( 'NONE',  ( 22.55334942336767767, 2.259292476615690770, 14.86850063742348915 ) ) ;
#76807=ORIENTED_EDGE ( 'NONE', *, *, #142991, .F. ) ;
#76808=FACE_OUTER_BOUND ( 'NONE', #15709, .T. ) ;
#76809=ORIENTED_EDGE ( 'NONE', *, *, #113509, .T. ) ;
#76810=LINE ( 'NONE', #120982, #71390 ) ;
#76812=ORIENTED_EDGE ( 'NONE', *, *, #29567, .T. ) ;
#76813=EDGE_LOOP ( 'NONE', ( #60059, #114971, #116483, #38981 ) ) ;
#76814=EDGE_CURVE ( 'NONE', #27100, #86567, #36934, .T. ) ;
#76815=DIRECTION ( 'NONE',  ( -0.7071067811865486830, 0.7071067811865464625, 0.000000000000000000 ) ) ;
#76816=DIRECTION ( 'NONE',  ( -0.000000000000000000, -0.3543493200069152693, 0.9351131265310292928 ) ) ;
#76817=CARTESIAN_POINT ( 'NONE',  ( -51.18398860626899705, 28.73617430169823095, 5.000000000000000000 ) ) ;
#76819=PLANE ( 'NONE',  #116866 ) ;
#76821=CARTESIAN_POINT ( 'NONE',  ( -34.92500000000001137, -22.22500000000000142, 4.000000000000000000 ) ) ;
#76823=CARTESIAN_POINT ( 'NONE',  ( -63.29974487139158867, -27.71228299555250274, 4.000000000000000000 ) ) ;
#76824=VECTOR ( 'NONE', #112508, 1000.000000000000000 ) ;
#76825=DIRECTION ( 'NONE',  ( -0.6830127018922181881, 0.6830127018922202975, -0.2588190451025214056 ) ) ;
#76827=CARTESIAN_POINT ( 'NONE',  ( -14.51078643762690490, -27.52281430457045275, 5.000000000000000000 ) ) ;
#76828=DIRECTION ( 'NONE',  ( 0.7071067811865487940, -0.7071067811865463515, 0.000000000000000000 ) ) ;
#76829=ADVANCED_FACE ( 'NONE', ( #70338 ), #16601, .F. ) ;
#76830=AXIS2_PLACEMENT_3D ( 'NONE', #102123, #123887, #24542 ) ;
#76831=ORIENTED_EDGE ( 'NONE', *, *, #64266, .F. ) ;
#76832=ORIENTED_EDGE ( 'NONE', *, *, #118328, .T. ) ;
#76833=ORIENTED_EDGE ( 'NONE', *, *, #76982, .F. ) ;
#76834=AXIS2_PLACEMENT_3D ( 'NONE', #136534, #5995, #14771 ) ;
#76835=DIRECTION ( 'NONE',  ( -0.3543493200069163240, -0.000000000000000000, -0.9351131265310288487 ) ) ;
#76836=VERTEX_POINT ( 'NONE', #47172 ) ;
#76837=ORIENTED_EDGE ( 'NONE', *, *, #92445, .F. ) ;
#76838=CARTESIAN_POINT ( 'NONE',  ( 23.99999999999983302, 13.55218569542903140, 5.000000000000000000 ) ) ;
#76840=EDGE_CURVE ( 'NONE', #19458, #34970, #68887, .T. ) ;
#76841=LINE ( 'NONE', #21712, #935 ) ;
#76842=CARTESIAN_POINT ( 'NONE',  ( -47.99451991528749062, 28.92564299267971251, 4.000000000000000000 ) ) ;
#76843=ORIENTED_EDGE ( 'NONE', *, *, #117609, .T. ) ;
#76844=PLANE ( 'NONE',  #27855 ) ;
#76845=VECTOR ( 'NONE', #51556, 999.9999999999998863 ) ;
#76846=VERTEX_POINT ( 'NONE', #13733 ) ;
#76849=ORIENTED_EDGE ( 'NONE', *, *, #34176, .F. ) ;
#76851=DIRECTION ( 'NONE',  ( -0.000000000000000000, -0.3543493200069152693, 0.9351131265310292928 ) ) ;
#76853=CARTESIAN_POINT ( 'NONE',  ( -27.52400138585429445, 22.03583458319438293, 4.979811245910086726 ) ) ;
#76854=ORIENTED_EDGE ( 'NONE', *, *, #102361, .T. ) ;
#76855=ORIENTED_EDGE ( 'NONE', *, *, #47697, .T. ) ;
#76856=ORIENTED_EDGE ( 'NONE', *, *, #48538, .F. ) ;
#76858=CARTESIAN_POINT ( 'NONE',  ( 6.328169399223490643, 20.25929247661551003, 4.000000000000000000 ) ) ;
#76859=CARTESIAN_POINT ( 'NONE',  ( 18.32816939922340183, -12.74070752338415247, 4.000000000000000000 ) ) ;
#76860=VECTOR ( 'NONE', #17619, 999.9999999999998863 ) ;
#76861=VECTOR ( 'NONE', #5089, 999.9999999999998863 ) ;
#76862=LINE ( 'NONE', #55813, #98316 ) ;
#76863=DIRECTION ( 'NONE',  ( -0.6830127018922180770, -0.6830127018922204085, -0.2588190451025213501 ) ) ;
#76864=ORIENTED_EDGE ( 'NONE', *, *, #114822, .F. ) ;
#76865=VECTOR ( 'NONE', #35998, 999.9999999999998863 ) ;
#76866=CARTESIAN_POINT ( 'NONE',  ( 29.99999999999978328, -5.527737879153164613, -7.983877177622441756 ) ) ;
#76867=AXIS2_PLACEMENT_3D ( 'NONE', #34889, #121147, #33474 ) ;
#76869=LINE ( 'NONE', #12279, #76766 ) ;
#76870=CARTESIAN_POINT ( 'NONE',  ( 6.183988606268994381, 28.73617430169791476, 5.000000000000000000 ) ) ;
#76871=ORIENTED_EDGE ( 'NONE', *, *, #128583, .T. ) ;
#76873=VECTOR ( 'NONE', #23723, 1000.000000000000000 ) ;
#76875=CARTESIAN_POINT ( 'NONE',  ( -45.29974487139158867, -27.71228299555237840, 4.000000000000000000 ) ) ;
#76878=CARTESIAN_POINT ( 'NONE',  ( 51.18398860626899705, 28.73617430169823095, 5.000000000000000000 ) ) ;
#76879=ORIENTED_EDGE ( 'NONE', *, *, #32505, .F. ) ;
#76880=ORIENTED_EDGE ( 'NONE', *, *, #43450, .T. ) ;
#76881=EDGE_CURVE ( 'NONE', #140719, #119697, #118025, .T. ) ;
#76882=LINE ( 'NONE', #134092, #53944 ) ;
#76883=DIRECTION ( 'NONE',  ( -0.7071067811865486830, -0.7071067811865464625, -0.000000000000000000 ) ) ;
#76885=DIRECTION ( 'NONE',  ( 0.6830127018922181881, 0.6830127018922202975, -0.2588190451025214056 ) ) ;
#76886=LINE ( 'NONE', #74736, #31329 ) ;
#76887=DIRECTION ( 'NONE',  ( 0.3543493200069162685, -0.000000000000000000, -0.9351131265310288487 ) ) ;
#76888=DIRECTION ( 'NONE',  ( 1.000000000000000000, 0.000000000000000000, 0.000000000000000000 ) ) ;
#76890=CARTESIAN_POINT ( 'NONE',  ( 57.18398860626899705, 28.73617430169827358, 5.000000000000000000 ) ) ;
#76891=DIRECTION ( 'NONE',  ( 0.6830127018922180770, -0.6830127018922204085, -0.2588190451025213501 ) ) ;
#76895=LINE ( 'NONE', #121068, #66853 ) ;
#76896=CARTESIAN_POINT ( 'NONE',  ( -34.45011844616455221, 7.516280811637403581, 5.000000000000000888 ) ) ;
#76897=DIRECTION ( 'NONE',  ( 0.7071067811865487940, 0.7071067811865463515, 0.000000000000000000 ) ) ;
#76898=VERTEX_POINT ( 'NONE', #139125 ) ;
#76899=EDGE_CURVE ( 'NONE', #71320, #57800, #107181, .T. ) ;
#76900=VECTOR ( 'NONE', #140420, 1000.000000000000000 ) ;
#76901=ORIENTED_EDGE ( 'NONE', *, *, #141278, .T. ) ;
#76903=VECTOR ( 'NONE', #76412, 1000.000000000000000 ) ;
#76904=ORIENTED_EDGE ( 'NONE', *, *, #24651, .T. ) ;
#76905=ORIENTED_EDGE ( 'NONE', *, *, #141990, .F. ) ;
#76907=EDGE_LOOP ( 'NONE', ( #129745, #123156, #106362, #121989 ) ) ;
#76908=LINE ( 'NONE', #40686, #110524 ) ;
#76909=DIRECTION ( 'NONE',  ( 0.6830127018922181881, 0.6830127018922202975, -0.2588190451025214056 ) ) ;
#76910=AXIS2_PLACEMENT_3D ( 'NONE', #95413, #56057, #12503 ) ;
#76911=ORIENTED_EDGE ( 'NONE', *, *, #95394, .F. ) ;
#76912=CARTESIAN_POINT ( 'NONE',  ( -21.29974487139158512, -27.71228299555221142, 4.000000000000000000 ) ) ;
#76913=CARTESIAN_POINT ( 'NONE',  ( -51.48921356237309510, -27.52281430457091460, 5.000000000000000000 ) ) ;
#76916=DIRECTION ( 'NONE',  ( 0.7071067811865486830, -0.7071067811865464625, -0.000000000000000000 ) ) ;
#76917=CARTESIAN_POINT ( 'NONE',  ( 0.000000000000000000, 0.000000000000000000, 5.000000000000000000 ) ) ;
#76918=CARTESIAN_POINT ( 'NONE',  ( -0.7067925072407263976, 20.25929247661552068, 20.83292124670814971 ) ) ;
#76920=FACE_OUTER_BOUND ( 'NONE', #126998, .T. ) ;
#76921=CARTESIAN_POINT ( 'NONE',  ( 20.51078643762690490, -27.52281430457041012, 5.000000000000000000 ) ) ;
#76923=DIRECTION ( 'NONE',  ( 0.7071067811865487940, 0.7071067811865463515, -0.000000000000000000 ) ) ;
#76924=VERTEX_POINT ( 'NONE', #95594 ) ;
#76925=ORIENTED_EDGE ( 'NONE', *, *, #138226, .F. ) ;
#76926=EDGE_CURVE ( 'NONE', #8478, #12275, #18730, .T. ) ;
#76928=ORIENTED_EDGE ( 'NONE', *, *, #125237, .T. ) ;
#76930=EDGE_CURVE ( 'NONE', #15696, #27121, #66382, .T. ) ;
#76931=VECTOR ( 'NONE', #40389, 999.9999999999998863 ) ;
#76932=CARTESIAN_POINT ( 'NONE',  ( -24.18398860626899705, 28.73617430169804265, 5.000000000000000000 ) ) ;
#76933=VECTOR ( 'NONE', #131235, 1000.000000000000000 ) ;
#76934=FACE_OUTER_BOUND ( 'NONE', #33170, .T. ) ;
#76936=EDGE_CURVE ( 'NONE', #133451, #14507, #96275, .T. ) ;
#76937=PLANE ( 'NONE',  #25876 ) ;
#76938=CARTESIAN_POINT ( 'NONE',  ( 50.99451991528749062, 28.92564299267973738, 4.000000000000000000 ) ) ;
#76941=ORIENTED_EDGE ( 'NONE', *, *, #123131, .T. ) ;
#76942=VECTOR ( 'NONE', #18871, 1000.000000000000000 ) ;
#76943=DIRECTION ( 'NONE',  ( 1.000000000000000000, 0.000000000000000000, 0.000000000000000000 ) ) ;
#76944=LINE ( 'NONE', #108070, #140408 ) ;
#76945=ORIENTED_EDGE ( 'NONE', *, *, #120725, .T. ) ;
#76946=EDGE_LOOP ( 'NONE', ( #77299, #95333, #100835, #130046 ) ) ;
#76948=EDGE_CURVE ( 'NONE', #62248, #76248, #30344, .T. ) ;
#76949=VERTEX_POINT ( 'NONE', #105733 ) ;
#76950=DIRECTION ( 'NONE',  ( 0.7071067811865486830, -0.7071067811865464625, -0.000000000000000000 ) ) ;
#76951=EDGE_CURVE ( 'NONE', #113958, #33777, #140520, .T. ) ;
#76953=VECTOR ( 'NONE', #66196, 1000.000000000000227 ) ;
#76958=ORIENTED_EDGE ( 'NONE', *, *, #73067, .F. ) ;
#76959=ORIENTED_EDGE ( 'NONE', *, *, #95678, .T. ) ;
#76960=VECTOR ( 'NONE', #119432, 1000.000000000000227 ) ;
#76961=EDGE_CURVE ( 'NONE', #84037, #123150, #128940, .T. ) ;
#76962=AXIS2_PLACEMENT_3D ( 'NONE', #10118, #87686, #3498 ) ;
#76963=EDGE_LOOP ( 'NONE', ( #32970, #102870, #85736, #93629 ) ) ;
#76964=AXIS2_PLACEMENT_3D ( 'NONE', #138440, #39128, #127558 ) ;
#76967=PLANE ( 'NONE',  #123254 ) ;
#76968=ORIENTED_EDGE ( 'NONE', *, *, #46994, .F. ) ;
#76969=CARTESIAN_POINT ( 'NONE',  ( -28.39656807105339453, -14.24070752338413648, 19.24067776001719210 ) ) ;
#76970=VECTOR ( 'NONE', #110386, 1000.000000000000227 ) ;
#76971=CARTESIAN_POINT ( 'NONE',  ( 16.49999999999988987, -10.91253812416064406, 4.000000000000000000 ) ) ;
#76976=FACE_BOUND ( 'NONE', #37571, .T. ) ;
#76977=EDGE_LOOP ( 'NONE', ( #58864, #382, #46164 ) ) ;
#76978=DIRECTION ( 'NONE',  ( -0.7071067811865486830, -0.7071067811865464625, 0.000000000000000000 ) ) ;
#76979=CARTESIAN_POINT ( 'NONE',  ( -5.292893218813420120, -15.74070752338412760, 5.000000000000000000 ) ) ;
#76981=ORIENTED_EDGE ( 'NONE', *, *, #10094, .F. ) ;
#76982=EDGE_CURVE ( 'NONE', #6466, #31236, #77281, .T. ) ;
#76983=CARTESIAN_POINT ( 'NONE',  ( -2.510786437626908008, -27.52281430457053446, 5.000000000000000000 ) ) ;
#76984=ORIENTED_EDGE ( 'NONE', *, *, #132325, .F. ) ;
#76985=EDGE_CURVE ( 'NONE', #26598, #128893, #73855, .T. ) ;
#76986=ORIENTED_EDGE ( 'NONE', *, *, #10941, .F. ) ;
#76988=ORIENTED_EDGE ( 'NONE', *, *, #84644, .F. ) ;
#76989=EDGE_CURVE ( 'NONE', #70885, #121450, #128248, .T. ) ;
#76991=VERTEX_POINT ( 'NONE', #17998 ) ;
#76992=CARTESIAN_POINT ( 'NONE',  ( -29.20666063542132207, 21.75929247661549226, 4.998822639870711626 ) ) ;
#76994=LINE ( 'NONE', #109579, #118190 ) ;
#76995=ORIENTED_EDGE ( 'NONE', *, *, #35308, .T. ) ;
#76996=VECTOR ( 'NONE', #138121, 1000.000000000000000 ) ;
#76997=FACE_OUTER_BOUND ( 'NONE', #54367, .T. ) ;
#76999=DIRECTION ( 'NONE',  ( 0.7071067811865487940, 0.7071067811865463515, 0.000000000000000000 ) ) ;
#77001=PLANE ( 'NONE',  #65587 ) ;
#77002=CARTESIAN_POINT ( 'NONE',  ( -8.999999999999932498, -3.033600742197707145, 5.000000000000000000 ) ) ;
#77004=ORIENTED_EDGE ( 'NONE', *, *, #70888, .F. ) ;
#77005=ORIENTED_EDGE ( 'NONE', *, *, #94890, .T. ) ;
#77007=DIRECTION ( 'NONE',  ( 0.7071067811865486830, -0.7071067811865464625, -0.000000000000000000 ) ) ;
#77008=DIRECTION ( 'NONE',  ( -0.7071067811865486830, -0.7071067811865464625, -0.000000000000000000 ) ) ;
#77009=VERTEX_POINT ( 'NONE', #106435 ) ;
#77010=ORIENTED_EDGE ( 'NONE', *, *, #39956, .F. ) ;
#77012=CARTESIAN_POINT ( 'NONE',  ( 0.000000000000000000, 0.000000000000000000, 5.000000000000000000 ) ) ;
#77013=DIRECTION ( 'NONE',  ( 0.7071067811865486830, -0.7071067811865464625, -0.000000000000000000 ) ) ;
#77014=VERTEX_POINT ( 'NONE', #143212 ) ;
#77015=DIRECTION ( 'NONE',  ( -0.3543493200069162685, -0.000000000000000000, -0.9351131265310288487 ) ) ;
#77019=EDGE_LOOP ( 'NONE', ( #90790, #22253, #37167, #4765 ) ) ;
#77021=CARTESIAN_POINT ( 'NONE',  ( 33.18398860626899705, 28.73617430169810305, 5.000000000000000000 ) ) ;
#77022=VECTOR ( 'NONE', #90276, 1000.000000000000227 ) ;
#77024=LINE ( 'NONE', #67577, #95791 ) ;
#77025=EDGE_LOOP ( 'NONE', ( #41610, #18799, #89954, #58542 ) ) ;
#77026=FACE_OUTER_BOUND ( 'NONE', #33837, .T. ) ;
#77027=VECTOR ( 'NONE', #7674, 999.9999999999998863 ) ;
#77029=LINE ( 'NONE', #46564, #19649 ) ;
#77030=DIRECTION ( 'NONE',  ( -0.7071067811865486830, 0.7071067811865464625, 0.000000000000000000 ) ) ;
#77031=CARTESIAN_POINT ( 'NONE',  ( 7.499999999999947597, 12.43112307739205846, 4.000000000000000000 ) ) ;
#77034=CARTESIAN_POINT ( 'NONE',  ( -25.49999999999982947, 16.18958161055400069, -11.56426086740816928 ) ) ;
#77037=LINE ( 'NONE', #21904, #50899 ) ;
#77038=LINE ( 'NONE', #109629, #83997 ) ;
#77039=ORIENTED_EDGE ( 'NONE', *, *, #5643, .T. ) ;
#77040=CARTESIAN_POINT ( 'NONE',  ( 2.816011393730999401, 28.73617430169785436, 5.000000000000000000 ) ) ;
#77041=ADVANCED_FACE ( 'NONE', ( #11231 ), #43914, .F. ) ;
#77042=LINE ( 'NONE', #56008, #108670 ) ;
#77043=VERTEX_POINT ( 'NONE', #94160 ) ;
#77044=EDGE_CURVE ( 'NONE', #69770, #43467, #127518, .T. ) ;
#77045=ORIENTED_EDGE ( 'NONE', *, *, #76222, .F. ) ;
#77046=VECTOR ( 'NONE', #118954, 1000.000000000000227 ) ;
#77047=DIRECTION ( 'NONE',  ( 0.6830127018922181881, 0.6830127018922202975, -0.2588190451025214056 ) ) ;
#77048=DIRECTION ( 'NONE',  ( -0.3543493200069162685, -0.000000000000000000, -0.9351131265310288487 ) ) ;
#77051=DIRECTION ( 'NONE',  ( -0.000000000000000000, -0.3543493200069152693, 0.9351131265310292928 ) ) ;
#77052=CARTESIAN_POINT ( 'NONE',  ( 24.29974487139158867, -27.71228299555223273, 4.000000000000000000 ) ) ;
#77053=VERTEX_POINT ( 'NONE', #61582 ) ;
#77054=EDGE_CURVE ( 'NONE', #36043, #32966, #73164, .T. ) ;
#77055=CARTESIAN_POINT ( 'NONE',  ( 30.79289321881324426, 15.75929247661555976, 5.000000000000000000 ) ) ;
#77056=DIRECTION ( 'NONE',  ( -0.7071067811865486830, -0.7071067811865464625, 0.000000000000000000 ) ) ;
#77057=LINE ( 'NONE', #120486, #3056 ) ;
#77058=VECTOR ( 'NONE', #67595, 999.9999999999998863 ) ;
#77061=DIRECTION ( 'NONE',  ( 1.000000000000000000, 0.000000000000000000, 0.000000000000000000 ) ) ;
#77063=EDGE_CURVE ( 'NONE', #100461, #58911, #84052, .T. ) ;
#77065=VERTEX_POINT ( 'NONE', #113421 ) ;
#77066=ORIENTED_EDGE ( 'NONE', *, *, #109631, .T. ) ;
#77067=LINE ( 'NONE', #24089, #37366 ) ;
#77068=ORIENTED_EDGE ( 'NONE', *, *, #86135, .T. ) ;
#77070=VECTOR ( 'NONE', #125206, 999.9999999999998863 ) ;
#77071=CARTESIAN_POINT ( 'NONE',  ( 11.99999999999991651, 2.966399257802230682, 5.000000000000000000 ) ) ;
#77072=CARTESIAN_POINT ( 'NONE',  ( -15.18398860626900237, 28.73617430169797871, 5.000000000000000000 ) ) ;
#77075=DIRECTION ( 'NONE',  ( -0.7071067811865486830, -0.7071067811865464625, 0.000000000000000000 ) ) ;
#77077=PLANE ( 'NONE',  #99541 ) ;
#77078=DIRECTION ( 'NONE',  ( -0.6830127018922180770, -0.6830127018922204085, -0.2588190451025213501 ) ) ;
#77080=ORIENTED_EDGE ( 'NONE', *, *, #10457, .F. ) ;
#77081=FACE_OUTER_BOUND ( 'NONE', #17807, .T. ) ;
#77082=CARTESIAN_POINT ( 'NONE',  ( -50.99451991528749062, 28.92564299267973738, 4.000000000000000000 ) ) ;
#77083=EDGE_CURVE ( 'NONE', #120068, #7267, #135905, .T. ) ;
#77084=LINE ( 'NONE', #45879, #114401 ) ;
#77085=CARTESIAN_POINT ( 'NONE',  ( -62.99451991528749772, 28.92564299267982264, 4.000000000000000000 ) ) ;
#77086=LINE ( 'NONE', #43711, #121444 ) ;
#77088=DIRECTION ( 'NONE',  ( -1.000000000000000000, 0.000000000000000000, 0.000000000000000000 ) ) ;
#77090=PLANE ( 'NONE',  #32928 ) ;
#77091=VECTOR ( 'NONE', #107673, 1000.000000000000000 ) ;
#77092=FACE_OUTER_BOUND ( 'NONE', #89844, .T. ) ;
#77093=VERTEX_POINT ( 'NONE', #12680 ) ;
#77094=VERTEX_POINT ( 'NONE', #24291 ) ;
#77096=CARTESIAN_POINT ( 'NONE',  ( 27.29974487139158512, -27.71228299555225405, 4.000000000000000000 ) ) ;
#77098=CARTESIAN_POINT ( 'NONE',  ( 3.005480084712505828, 28.92564299267936079, 4.000000000000000000 ) ) ;
#77099=ORIENTED_EDGE ( 'NONE', *, *, #51236, .F. ) ;
#77100=CARTESIAN_POINT ( 'NONE',  ( 45.18398860626900415, 28.73617430169818832, 5.000000000000000000 ) ) ;
#77101=AXIS2_PLACEMENT_3D ( 'NONE', #82508, #128166, #6305 ) ;
#77102=DIRECTION ( 'NONE',  ( -0.000000000000000000, -0.3543493200069152693, 0.9351131265310292928 ) ) ;
#77104=ADVANCED_FACE ( 'NONE', ( #14106 ), #124311, .T. ) ;
#77106=VECTOR ( 'NONE', #19925, 1000.000000000000227 ) ;
#77107=ORIENTED_EDGE ( 'NONE', *, *, #32275, .T. ) ;
#77109=ORIENTED_EDGE ( 'NONE', *, *, #124211, .T. ) ;
#77110=ORIENTED_EDGE ( 'NONE', *, *, #113838, .F. ) ;
#77112=CARTESIAN_POINT ( 'NONE',  ( 5.999999999999956479, -7.068876922607745250, 4.000000000000000000 ) ) ;
#77114=LINE ( 'NONE', #8214, #103249 ) ;
#77115=CARTESIAN_POINT ( 'NONE',  ( 34.82816939922329880, -17.24070752338409562, 4.000000000000000000 ) ) ;
#77116=CARTESIAN_POINT ( 'NONE',  ( 66.48921356237309510, -27.52281430457101763, 5.000000000000000000 ) ) ;
#77117=EDGE_LOOP ( 'NONE', ( #100093, #103917, #82480, #21853 ) ) ;
#77118=ADVANCED_FACE ( 'NONE', ( #88859 ), #90999, .F. ) ;
#77121=VERTEX_POINT ( 'NONE', #135223 ) ;
#77123=EDGE_CURVE ( 'NONE', #73032, #26933, #79439, .T. ) ;
#77126=LINE ( 'NONE', #65544, #30053 ) ;
#77127=VECTOR ( 'NONE', #126746, 1000.000000000000000 ) ;
#77128=VERTEX_POINT ( 'NONE', #56256 ) ;
#77129=ADVANCED_FACE ( 'NONE', ( #1083 ), #69238, .T. ) ;
#77130=FACE_OUTER_BOUND ( 'NONE', #125196, .T. ) ;
#77133=VECTOR ( 'NONE', #113283, 1000.000000000000000 ) ;
#77134=CARTESIAN_POINT ( 'NONE',  ( -18.15612307739227660, -22.22499999999999432, 4.000000000000000000 ) ) ;
#77135=CARTESIAN_POINT ( 'NONE',  ( 54.48921356237310221, -27.52281430457093236, 5.000000000000000000 ) ) ;
#77136=ORIENTED_EDGE ( 'NONE', *, *, #71843, .F. ) ;
#77137=ORIENTED_EDGE ( 'NONE', *, *, #61436, .T. ) ;
#77141=ORIENTED_EDGE ( 'NONE', *, *, #121744, .F. ) ;
#77142=( BOUNDED_CURVE ( )  B_SPLINE_CURVE ( 3, ( #140057, #128459, #41426, #52302 ),
 .UNSPECIFIED., .F., .F. ) 
 B_SPLINE_CURVE_WITH_KNOTS ( ( 4, 4 ),
 ( 5.005968288816727174, 5.074607125596338086 ),
 .UNSPECIFIED. ) 
 CURVE ( )  GEOMETRIC_REPRESENTATION_ITEM ( )  RATIONAL_B_SPLINE_CURVE ( ( 1.000000000000000000, 0.9996074310407765395, 0.9996074310407765395, 1.000000000000000000 ) ) 
 REPRESENTATION_ITEM ( '' )  );
#77144=LINE ( 'NONE', #98155, #60667 ) ;
#77145=VERTEX_POINT ( 'NONE', #80831 ) ;
#77146=CARTESIAN_POINT ( 'NONE',  ( -30.18398860626900060, 28.73617430169808173, 5.000000000000000000 ) ) ;
#77148=AXIS2_PLACEMENT_3D ( 'NONE', #135699, #56753, #36385 ) ;
#77151=FACE_BOUND ( 'NONE', #50066, .T. ) ;
#77152=FACE_OUTER_BOUND ( 'NONE', #131087, .T. ) ;
#77153=DIRECTION ( 'NONE',  ( -0.000000000000000000, -0.000000000000000000, 1.000000000000000000 ) ) ;
#77156=ORIENTED_EDGE ( 'NONE', *, *, #130827, .T. ) ;
#77157=PLANE ( 'NONE',  #106552 ) ;
#77158=EDGE_LOOP ( 'NONE', ( #98837, #5460, #107198, #74734 ) ) ;
#77159=ADVANCED_FACE ( 'NONE', ( #67093 ), #111277, .F. ) ;
#77163=ORIENTED_EDGE ( 'NONE', *, *, #106659, .F. ) ;
#77165=DIRECTION ( 'NONE',  ( 0.6830127018922181881, 0.6830127018922202975, -0.2588190451025214056 ) ) ;
#77166=ORIENTED_EDGE ( 'NONE', *, *, #41911, .T. ) ;
#77167=DIRECTION ( 'NONE',  ( -0.7071067811865486830, 0.7071067811865464625, 0.000000000000000000 ) ) ;
#77168=VECTOR ( 'NONE', #104999, 1000.000000000000114 ) ;
#77173=LINE ( 'NONE', #8964, #32020 ) ;
#77174=FACE_OUTER_BOUND ( 'NONE', #97774, .T. ) ;
#77175=DIRECTION ( 'NONE',  ( -0.3543493200069163240, 0.000000000000000000, -0.9351131265310288487 ) ) ;
#77176=ORIENTED_EDGE ( 'NONE', *, *, #69066, .F. ) ;
#77177=AXIS2_PLACEMENT_3D ( 'NONE', #50262, #138704, #39388 ) ;
#77179=LINE ( 'NONE', #120618, #9792 ) ;
#77182=VECTOR ( 'NONE', #140777, 1000.000000000000227 ) ;
#77183=ORIENTED_EDGE ( 'NONE', *, *, #133552, .T. ) ;
#77184=ORIENTED_EDGE ( 'NONE', *, *, #64760, .T. ) ;
#77186=ORIENTED_EDGE ( 'NONE', *, *, #44479, .T. ) ;
#77187=DIRECTION ( 'NONE',  ( -0.7071067811865486830, 0.7071067811865464625, 0.000000000000000000 ) ) ;
#77188=CARTESIAN_POINT ( 'NONE',  ( -2.700255128608413990, -27.71228299555204089, 4.000000000000000000 ) ) ;
#77189=VECTOR ( 'NONE', #78466, 1000.000000000000000 ) ;
#77191=LINE ( 'NONE', #79350, #107434 ) ;
#77192=ORIENTED_EDGE ( 'NONE', *, *, #51685, .F. ) ;
#77193=DIRECTION ( 'NONE',  ( -0.000000000000000000, 0.000000000000000000, 1.000000000000000000 ) ) ;
#77194=ORIENTED_EDGE ( 'NONE', *, *, #98533, .T. ) ;
#77197=PLANE ( 'NONE',  #28967 ) ;
#77198=DIRECTION ( 'NONE',  ( 0.6830127018922181881, 0.6830127018922202975, -0.2588190451025214056 ) ) ;
#77199=ORIENTED_EDGE ( 'NONE', *, *, #95577, .F. ) ;
#77201=DIRECTION ( 'NONE',  ( -0.6830127018922181881, 0.6830127018922202975, -0.2588190451025214056 ) ) ;
#77203=VECTOR ( 'NONE', #20622, 1000.000000000000000 ) ;
#77205=DIRECTION ( 'NONE',  ( -0.000000000000000000, 0.000000000000000000, 1.000000000000000000 ) ) ;
#77206=ORIENTED_EDGE ( 'NONE', *, *, #14967, .T. ) ;
#77207=VECTOR ( 'NONE', #100360, 1000.000000000000000 ) ;
#77208=CARTESIAN_POINT ( 'NONE',  ( 12.18398860626900060, 28.73617430169795739, 5.000000000000000000 ) ) ;
#77209=CARTESIAN_POINT ( 'NONE',  ( 34.92499999999998295, 11.81665438641033106, 4.500000000000000888 ) ) ;
#77210=PLANE ( 'NONE',  #50795 ) ;
#77212=CARTESIAN_POINT ( 'NONE',  ( 48.18398860626899705, 28.73617430169820608, 5.000000000000000000 ) ) ;
#77213=VECTOR ( 'NONE', #135850, 999.9999999999998863 ) ;
#77214=EDGE_CURVE ( 'NONE', #63923, #25547, #46761, .T. ) ;
#77215=CARTESIAN_POINT ( 'NONE',  ( 5.292893218813423672, -12.74070752338415247, 5.000000000000000000 ) ) ;
#77217=EDGE_CURVE ( 'NONE', #99583, #75231, #50331, .T. ) ;
#77218=EDGE_CURVE ( 'NONE', #28732, #9245, #59789, .T. ) ;
#77219=ORIENTED_EDGE ( 'NONE', *, *, #8112, .F. ) ;
#77220=DIRECTION ( 'NONE',  ( 0.3543493200069162685, -0.000000000000000000, -0.9351131265310288487 ) ) ;
#77221=ORIENTED_EDGE ( 'NONE', *, *, #141493, .T. ) ;
#77223=VECTOR ( 'NONE', #48974, 1000.000000000000114 ) ;
#77225=EDGE_CURVE ( 'NONE', #70402, #137770, #127154, .T. ) ;
#77227=DIRECTION ( 'NONE',  ( 1.000000000000000000, 0.000000000000000000, 0.000000000000000000 ) ) ;
#77228=AXIS2_PLACEMENT_3D ( 'NONE', #71485, #7621, #16344 ) ;
#77230=CARTESIAN_POINT ( 'NONE',  ( 21.18398860626899349, 28.73617430169802134, 5.000000000000000000 ) ) ;
#77231=CARTESIAN_POINT ( 'NONE',  ( 16.49999999999988276, -17.56887692260763956, 4.000000000000000000 ) ) ;
#77232=LINE ( 'NONE', #66342, #120790 ) ;
#77233=ORIENTED_EDGE ( 'NONE', *, *, #22533, .F. ) ;
#77235=DIRECTION ( 'NONE',  ( 0.6830127018922180770, -0.6830127018922204085, -0.2588190451025213501 ) ) ;
#77237=LINE ( 'NONE', #55460, #35398 ) ;
#77240=PLANE ( 'NONE',  #69072 ) ;
#77242=FACE_OUTER_BOUND ( 'NONE', #59473, .T. ) ;
#77243=EDGE_CURVE ( 'NONE', #75031, #10935, #16985, .T. ) ;
#77244=LINE ( 'NONE', #45330, #131841 ) ;
#77245=CARTESIAN_POINT ( 'NONE',  ( -1.499999999999987566, 0.4497235411627421575, -5.599840258123544245 ) ) ;
#77246=LINE ( 'NONE', #22095, #69624 ) ;
#77247=ORIENTED_EDGE ( 'NONE', *, *, #103549, .T. ) ;
#77248=CARTESIAN_POINT ( 'NONE',  ( 31.17183060077625356, 12.75929247661558286, 4.000000000000000000 ) ) ;
#77249=ORIENTED_EDGE ( 'NONE', *, *, #136603, .F. ) ;
#77251=CARTESIAN_POINT ( 'NONE',  ( -20.99999999999985789, -8.151047557385087572, -8.977947279169748995 ) ) ;
#77252=LINE ( 'NONE', #43174, #56947 ) ;
#77255=DIRECTION ( 'NONE',  ( -1.000000000000000000, 0.000000000000000000, 0.000000000000000000 ) ) ;
#77256=LINE ( 'NONE', #33741, #69366 ) ;
#77257=CARTESIAN_POINT ( 'NONE',  ( -34.45011844616454511, 13.51628081163733874, 5.000000000000000888 ) ) ;
#77258=DIRECTION ( 'NONE',  ( -0.000000000000000000, 0.000000000000000000, 1.000000000000000000 ) ) ;
#77259=EDGE_LOOP ( 'NONE', ( #83189, #135690, #27664, #25562 ) ) ;
#77260=AXIS2_PLACEMENT_3D ( 'NONE', #142533, #120010, #43220 ) ;
#77261=ORIENTED_EDGE ( 'NONE', *, *, #128318, .F. ) ;
#77262=LINE ( 'NONE', #121430, #74190 ) ;
#77263=EDGE_CURVE ( 'NONE', #5121, #142121, #136604, .T. ) ;
#77264=DIRECTION ( 'NONE',  ( 0.3543493200069163240, 0.000000000000000000, -0.9351131265310288487 ) ) ;
#77265=DIRECTION ( 'NONE',  ( 0.000000000000000000, 0.000000000000000000, 1.000000000000000000 ) ) ;
#77267=LINE ( 'NONE', #109855, #143485 ) ;
#77268=VECTOR ( 'NONE', #68619, 1000.000000000000000 ) ;
#77269=LINE ( 'NONE', #52613, #76163 ) ;
#77270=ORIENTED_EDGE ( 'NONE', *, *, #34201, .F. ) ;
#77272=CARTESIAN_POINT ( 'NONE',  ( 25.49999999999982947, -20.94781430457061333, 5.000000000000000000 ) ) ;
#77273=LINE ( 'NONE', #85971, #92391 ) ;
#77274=PLANE ( 'NONE',  #19647 ) ;
#77275=EDGE_CURVE ( 'NONE', #36187, #79492, #61938, .T. ) ;
#77276=VERTEX_POINT ( 'NONE', #48913 ) ;
#77277=AXIS2_PLACEMENT_3D ( 'NONE', #130992, #52686, #20772 ) ;
#77278=DIRECTION ( 'NONE',  ( -0.000000000000000000, 0.3543493200069153248, 0.9351131265310292928 ) ) ;
#77280=ORIENTED_EDGE ( 'NONE', *, *, #59863, .T. ) ;
#77281=LINE ( 'NONE', #121452, #44241 ) ;
#77283=EDGE_CURVE ( 'NONE', #105795, #61439, #126644, .T. ) ;
#77284=DIRECTION ( 'NONE',  ( -0.7071067811865486830, -0.7071067811865464625, 0.000000000000000000 ) ) ;
#77285=ORIENTED_EDGE ( 'NONE', *, *, #81199, .F. ) ;
#77286=DIRECTION ( 'NONE',  ( 0.6830127018922181881, 0.6830127018922202975, -0.2588190451025214056 ) ) ;
#77287=EDGE_CURVE ( 'NONE', #31893, #135641, #72844, .T. ) ;
#77288=CARTESIAN_POINT ( 'NONE',  ( 3.299744871391591339, -27.71228299555208352, 4.000000000000000000 ) ) ;
#77289=DIRECTION ( 'NONE',  ( 0.7071067811865487940, 0.7071067811865463515, -0.000000000000000000 ) ) ;
#77290=CARTESIAN_POINT ( 'NONE',  ( 42.29974487139158157, -27.71228299555235708, 4.000000000000000000 ) ) ;
#77291=PLANE ( 'NONE',  #81040 ) ;
#77293=ORIENTED_EDGE ( 'NONE', *, *, #10680, .T. ) ;
#77295=CARTESIAN_POINT ( 'NONE',  ( -15.12147316337138214, -20.24070752338408141, 7.412974875817823772 ) ) ;
#77296=CARTESIAN_POINT ( 'NONE',  ( -21.46160355370557582, -9.740707523384180888, 17.74957260769605938 ) ) ;
#77297=AXIS2_PLACEMENT_3D ( 'NONE', #6646, #119019, #119702 ) ;
#77298=DIRECTION ( 'NONE',  ( -0.7071067811865486830, -0.7071067811865464625, 0.000000000000000000 ) ) ;
#77299=ORIENTED_EDGE ( 'NONE', *, *, #96963, .T. ) ;
#77300=ORIENTED_EDGE ( 'NONE', *, *, #27077, .F. ) ;
#77302=VECTOR ( 'NONE', #121063, 1000.000000000000000 ) ;
#77303=EDGE_LOOP ( 'NONE', ( #134146, #95247, #50790, #131952 ) ) ;
#77305=CARTESIAN_POINT ( 'NONE',  ( 21.79289321881330466, 12.75929247661559351, 5.000000000000000000 ) ) ;
#77306=CARTESIAN_POINT ( 'NONE',  ( -20.99999999999985079, -0.2811185226894475919, -5.995736974527464902 ) ) ;
#77307=CARTESIAN_POINT ( 'NONE',  ( -34.42500000000001137, -22.22500000000000142, 5.000000000000000000 ) ) ;
#77308=PLANE ( 'NONE',  #10921 ) ;
#77309=DIRECTION ( 'NONE',  ( 1.000000000000000000, -0.000000000000000000, 0.000000000000000000 ) ) ;
#77310=ORIENTED_EDGE ( 'NONE', *, *, #18036, .T. ) ;
#77311=EDGE_LOOP ( 'NONE', ( #64131, #96861, #62181, #107658 ) ) ;
#77312=DIRECTION ( 'NONE',  ( -0.7071067811865487940, 0.7071067811865463515, -0.000000000000000000 ) ) ;
#77313=DIRECTION ( 'NONE',  ( 0.7071067811865486830, -0.7071067811865464625, -0.000000000000000000 ) ) ;
#77314=VECTOR ( 'NONE', #24913, 1000.000000000000000 ) ;
#77317=VECTOR ( 'NONE', #47287, 1000.000000000000000 ) ;
#77318=DIRECTION ( 'NONE',  ( 0.3543493200069162685, -0.000000000000000000, -0.9351131265310288487 ) ) ;
#77320=CARTESIAN_POINT ( 'NONE',  ( -0.1839886062690032631, 28.73617430169787568, 5.000000000000000000 ) ) ;
#77322=ORIENTED_EDGE ( 'NONE', *, *, #88400, .F. ) ;
#77323=VECTOR ( 'NONE', #137753, 1000.000000000000000 ) ;
#77324=EDGE_CURVE ( 'NONE', #62339, #79834, #5363, .T. ) ;
#77325=DIRECTION ( 'NONE',  ( -0.7071067811865486830, 0.7071067811865464625, 0.000000000000000000 ) ) ;
#77326=LINE ( 'NONE', #119337, #22266 ) ;
#77327=DIRECTION ( 'NONE',  ( -0.7071067811865486830, -0.7071067811865464625, 0.000000000000000000 ) ) ;
#77328=PLANE ( 'NONE',  #89972 ) ;
#77329=LINE ( 'NONE', #58450, #64239 ) ;
#77330=VECTOR ( 'NONE', #50469, 1000.000000000000000 ) ;
#77334=ORIENTED_EDGE ( 'NONE', *, *, #4471, .T. ) ;
#77335=EDGE_CURVE ( 'NONE', #3406, #126947, #82959, .T. ) ;
#77336=VECTOR ( 'NONE', #122428, 1000.000000000000227 ) ;
#77337=ORIENTED_EDGE ( 'NONE', *, *, #1709, .F. ) ;
#77339=ORIENTED_EDGE ( 'NONE', *, *, #83627, .F. ) ;
#77340=ORIENTED_EDGE ( 'NONE', *, *, #95735, .F. ) ;
#77341=AXIS2_PLACEMENT_3D ( 'NONE', #70131, #94666, #39624 ) ;
#77342=FACE_OUTER_BOUND ( 'NONE', #78989, .T. ) ;
#77343=EDGE_CURVE ( 'NONE', #32288, #130620, #61042, .T. ) ;
#77344=CARTESIAN_POINT ( 'NONE',  ( 13.04515773336657780, -21.74070752338407075, 21.72585301388587808 ) ) ;
#77345=LINE ( 'NONE', #99032, #123589 ) ;
#77346=EDGE_CURVE ( 'NONE', #22185, #19349, #138554, .T. ) ;
#77347=ORIENTED_EDGE ( 'NONE', *, *, #49440, .T. ) ;
#77348=CARTESIAN_POINT ( 'NONE',  ( -48.48921356237309510, -27.52281430457089328, 5.000000000000000000 ) ) ;
#77350=DIRECTION ( 'NONE',  ( 0.7071067811865487940, -0.7071067811865463515, 0.000000000000000000 ) ) ;
#77351=DIRECTION ( 'NONE',  ( -0.000000000000000000, 0.3543493200069153248, 0.9351131265310292928 ) ) ;
#77352=FACE_OUTER_BOUND ( 'NONE', #94781, .T. ) ;
#77356=ORIENTED_EDGE ( 'NONE', *, *, #451, .F. ) ;
#77358=CARTESIAN_POINT ( 'NONE',  ( 0.000000000000000000, 0.000000000000000000, 5.000000000000000000 ) ) ;
#77359=ORIENTED_EDGE ( 'NONE', *, *, #130494, .T. ) ;
#77360=ORIENTED_EDGE ( 'NONE', *, *, #135797, .T. ) ;
#77362=VERTEX_POINT ( 'NONE', #72629 ) ;
#77364=EDGE_LOOP ( 'NONE', ( #43827, #39541, #60099, #96383 ) ) ;
#77366=VECTOR ( 'NONE', #80749, 1000.000000000000000 ) ;
#77369=CARTESIAN_POINT ( 'NONE',  ( 30.98911971346031180, -22.02621442084248216, 4.990779571109225543 ) ) ;
#77370=ORIENTED_EDGE ( 'NONE', *, *, #59022, .F. ) ;
#77372=CARTESIAN_POINT ( 'NONE',  ( 1.499999999999997780, 7.466399257802191158, 5.000000000000000000 ) ) ;
#77373=VECTOR ( 'NONE', #41458, 1000.000000000000000 ) ;
#77374=CARTESIAN_POINT ( 'NONE',  ( 12.00548008471251293, 28.92564299267929684, 4.000000000000000000 ) ) ;
#77375=CARTESIAN_POINT ( 'NONE',  ( 0.000000000000000000, 0.000000000000000000, 5.000000000000000000 ) ) ;
#77376=EDGE_LOOP ( 'NONE', ( #77163, #126515, #31634, #65685 ) ) ;
#77377=CARTESIAN_POINT ( 'NONE',  ( 30.79333936457826937, 21.75929247661550647, 4.998822639870708073 ) ) ;
#77378=ORIENTED_EDGE ( 'NONE', *, *, #69339, .T. ) ;
#77379=VERTEX_POINT ( 'NONE', #39984 ) ;
#77380=ORIENTED_EDGE ( 'NONE', *, *, #62018, .T. ) ;
#77382=ADVANCED_FACE ( 'NONE', ( #129805 ), #39250, .F. ) ;
#77383=CARTESIAN_POINT ( 'NONE',  ( 10.17183060077640810, 3.759292476615685441, 4.000000000000000000 ) ) ;
#77384=CARTESIAN_POINT ( 'NONE',  ( 19.17183060077634238, -11.24070752338416490, 4.000000000000000000 ) ) ;
#77385=EDGE_CURVE ( 'NONE', #45976, #22044, #27629, .T. ) ;
#77386=EDGE_CURVE ( 'NONE', #88378, #70323, #140000, .T. ) ;
#77387=ORIENTED_EDGE ( 'NONE', *, *, #62067, .F. ) ;
#77390=EDGE_CURVE ( 'NONE', #103866, #129269, #74012, .T. ) ;
#77391=EDGE_CURVE ( 'NONE', #19406, #75708, #38524, .T. ) ;
#77394=CARTESIAN_POINT ( 'NONE',  ( 30.18398860626900060, 28.73617430169808173, 5.000000000000000000 ) ) ;
#77396=DIRECTION ( 'NONE',  ( 0.7071067811865487940, 0.7071067811865463515, -0.000000000000000000 ) ) ;
#77397=CARTESIAN_POINT ( 'NONE',  ( -12.47512612785037689, 14.25929247661557397, 9.797011795316608485 ) ) ;
#77398=ORIENTED_EDGE ( 'NONE', *, *, #24340, .F. ) ;
#77399=VERTEX_POINT ( 'NONE', #83463 ) ;
#77400=ADVANCED_FACE ( 'NONE', ( #62434 ), #73307, .T. ) ;
#77401=ORIENTED_EDGE ( 'NONE', *, *, #34040, .F. ) ;
#77403=FACE_OUTER_BOUND ( 'NONE', #36483, .T. ) ;
#77404=EDGE_CURVE ( 'NONE', #54347, #132587, #82750, .T. ) ;
#77405=CARTESIAN_POINT ( 'NONE',  ( -18.79289321881332597, -11.24070752338416668, 5.000000000000000000 ) ) ;
#77406=DIRECTION ( 'NONE',  ( -0.000000000000000000, 0.000000000000000000, 1.000000000000000000 ) ) ;
#77407=ADVANCED_FACE ( 'NONE', ( #6548 ), #63164, .T. ) ;
#77410=DIRECTION ( 'NONE',  ( 0.7071067811865487940, 0.7071067811865463515, 0.000000000000000000 ) ) ;
#77411=DIRECTION ( 'NONE',  ( 0.3543493200069163240, 0.000000000000000000, 0.9351131265310288487 ) ) ;
#77412=PLANE ( 'NONE',  #23491 ) ;
#77413=EDGE_LOOP ( 'NONE', ( #132836, #92072, #24012, #52873 ) ) ;
#77414=DIRECTION ( 'NONE',  ( 1.000000000000000000, 0.000000000000000000, 0.000000000000000000 ) ) ;
#77415=ORIENTED_EDGE ( 'NONE', *, *, #22805, .F. ) ;
#77416=DIRECTION ( 'NONE',  ( 0.7071067811865487940, 0.7071067811865463515, 0.000000000000000000 ) ) ;
#77418=EDGE_CURVE ( 'NONE', #136567, #16596, #8007, .T. ) ;
#77421=VERTEX_POINT ( 'NONE', #106591 ) ;
#77422=VECTOR ( 'NONE', #60263, 1000.000000000000227 ) ;
#77423=CARTESIAN_POINT ( 'NONE',  ( -17.70025512860841488, -27.71228299555193786, 4.000000000000000000 ) ) ;
#77424=EDGE_LOOP ( 'NONE', ( #97249, #13526, #52279, #101179 ) ) ;
#77426=VERTEX_POINT ( 'NONE', #7289 ) ;
#77428=ORIENTED_EDGE ( 'NONE', *, *, #55838, .F. ) ;
#77430=VECTOR ( 'NONE', #5807, 1000.000000000000000 ) ;
#77434=CARTESIAN_POINT ( 'NONE',  ( -27.70710678118634362, -18.74070752338409207, 5.000000000000000000 ) ) ;
#77437=DIRECTION ( 'NONE',  ( -0.7071067811865487940, 0.7071067811865463515, 0.000000000000000000 ) ) ;
#77440=FACE_OUTER_BOUND ( 'NONE', #107550, .T. ) ;
#77441=CARTESIAN_POINT ( 'NONE',  ( -33.48921356237309510, -27.52281430457078670, 5.000000000000000000 ) ) ;
#77442=ORIENTED_EDGE ( 'NONE', *, *, #79555, .T. ) ;
#77443=VERTEX_POINT ( 'NONE', #129087 ) ;
#77444=AXIS2_PLACEMENT_3D ( 'NONE', #97439, #65592, #87307 ) ;
#77445=DIRECTION ( 'NONE',  ( 0.7071067811865486830, -0.7071067811865464625, -0.000000000000000000 ) ) ;
#77446=EDGE_LOOP ( 'NONE', ( #140045, #60775, #131157, #52485 ) ) ;
#77447=EDGE_CURVE ( 'NONE', #108671, #78331, #18899, .T. ) ;
#77449=CARTESIAN_POINT ( 'NONE',  ( 29.29298673570674438, -21.74070752338405654, 4.999753212805219782 ) ) ;
#77450=DIRECTION ( 'NONE',  ( 0.7071067811865486830, -0.7071067811865464625, -0.000000000000000000 ) ) ;
#77452=ORIENTED_EDGE ( 'NONE', *, *, #117429, .F. ) ;
#77453=LINE ( 'NONE', #79619, #93818 ) ;
#77454=DIRECTION ( 'NONE',  ( -0.6830127018922181881, 0.6830127018922202975, -0.2588190451025214056 ) ) ;
#77456=DIRECTION ( 'NONE',  ( 0.7071067811865487940, 0.7071067811865463515, -0.000000000000000000 ) ) ;
#77459=DIRECTION ( 'NONE',  ( -0.7071067811865486830, 0.7071067811865464625, 0.000000000000000000 ) ) ;
#77461=LINE ( 'NONE', #99146, #67811 ) ;
#77462=CARTESIAN_POINT ( 'NONE',  ( -71.99451991528749772, 28.92564299267988304, 4.000000000000000000 ) ) ;
#77463=LINE ( 'NONE', #121626, #22408 ) ;
#77464=FACE_OUTER_BOUND ( 'NONE', #9506, .T. ) ;
#77465=VERTEX_POINT ( 'NONE', #141398 ) ;
#77466=ORIENTED_EDGE ( 'NONE', *, *, #107976, .T. ) ;
#77469=ORIENTED_EDGE ( 'NONE', *, *, #20389, .T. ) ;
#77470=ADVANCED_FACE ( 'NONE', ( #33399 ), #31929, .F. ) ;
#77472=LINE ( 'NONE', #97760, #128801 ) ;
#77476=VECTOR ( 'NONE', #131888, 1000.000000000000000 ) ;
#77478=ORIENTED_EDGE ( 'NONE', *, *, #98881, .T. ) ;
#77479=CARTESIAN_POINT ( 'NONE',  ( -14.99999999999989519, -7.068876922607736368, 4.000000000000000000 ) ) ;
#77481=VERTEX_POINT ( 'NONE', #9415 ) ;
#77483=EDGE_CURVE ( 'NONE', #81979, #23623, #8688, .T. ) ;
#77484=ORIENTED_EDGE ( 'NONE', *, *, #141290, .F. ) ;
#77485=FACE_OUTER_BOUND ( 'NONE', #85040, .T. ) ;
#77486=EDGE_CURVE ( 'NONE', #99307, #566, #11566, .T. ) ;
#77487=FACE_OUTER_BOUND ( 'NONE', #136239, .T. ) ;
#77489=CARTESIAN_POINT ( 'NONE',  ( 23.99999999999984723, -16.44781430457065241, 5.000000000000000000 ) ) ;
#77490=VECTOR ( 'NONE', #40788, 1000.000000000000227 ) ;
#77491=CARTESIAN_POINT ( 'NONE',  ( -25.49999999999982236, 13.56627193232212392, -10.57019076586074391 ) ) ;
#77492=CARTESIAN_POINT ( 'NONE',  ( 34.42499999999998295, 11.97718569542927014, 5.000000000000000000 ) ) ;
#77493=DIRECTION ( 'NONE',  ( -0.7071067811865486830, 0.7071067811865464625, 0.000000000000000000 ) ) ;
#77494=AXIS2_PLACEMENT_3D ( 'NONE', #63885, #31253, #53725 ) ;
#77495=EDGE_CURVE ( 'NONE', #136084, #39996, #142141, .T. ) ;
#77496=ORIENTED_EDGE ( 'NONE', *, *, #3092, .F. ) ;
#77497=ORIENTED_EDGE ( 'NONE', *, *, #50418, .T. ) ;
#77499=CARTESIAN_POINT ( 'NONE',  ( -20.18650864602349060, -15.74070752338412404, 8.904080028138988467 ) ) ;
#77500=VERTEX_POINT ( 'NONE', #31229 ) ;
#77501=ORIENTED_EDGE ( 'NONE', *, *, #113153, .T. ) ;
#77502=ADVANCED_FACE ( 'NONE', ( #66705 ), #20311, .F. ) ;
#77503=DIRECTION ( 'NONE',  ( 0.7071067811865487940, 0.7071067811865463515, 0.000000000000000000 ) ) ;
#77504=EDGE_CURVE ( 'NONE', #31910, #56980, #99295, .T. ) ;
#77505=VERTEX_POINT ( 'NONE', #42826 ) ;
#77506=VECTOR ( 'NONE', #16004, 999.9999999999998863 ) ;
#77507=CARTESIAN_POINT ( 'NONE',  ( -26.99999999999981526, -13.39766691384885711, -10.96608748226459618 ) ) ;
#77508=LINE ( 'NONE', #55028, #43909 ) ;
#77510=DIRECTION ( 'NONE',  ( -0.000000000000000000, 0.000000000000000000, 1.000000000000000000 ) ) ;
#77511=LINE ( 'NONE', #109391, #79085 ) ;
#77512=ORIENTED_EDGE ( 'NONE', *, *, #118260, .F. ) ;
#77515=CARTESIAN_POINT ( 'NONE',  ( 28.49999999999980460, 18.05218569542898521, 5.000000000000000000 ) ) ;
#77517=LINE ( 'NONE', #134759, #83906 ) ;
#77518=EDGE_CURVE ( 'NONE', #131139, #92065, #131973, .T. ) ;
#77519=ORIENTED_EDGE ( 'NONE', *, *, #95363, .F. ) ;
#77520=PLANE ( 'NONE',  #4141 ) ;
#77521=ORIENTED_EDGE ( 'NONE', *, *, #53833, .T. ) ;
#77522=ORIENTED_EDGE ( 'NONE', *, *, #33738, .T. ) ;
#77523=ORIENTED_EDGE ( 'NONE', *, *, #56396, .T. ) ;
#77524=DIRECTION ( 'NONE',  ( 0.6830127018922180770, -0.6830127018922204085, -0.2588190451025213501 ) ) ;
#77525=LINE ( 'NONE', #78955, #8132 ) ;
#77526=VECTOR ( 'NONE', #44403, 1000.000000000000000 ) ;
#77527=VECTOR ( 'NONE', #107125, 999.9999999999998863 ) ;
#77529=PLANE ( 'NONE',  #70414 ) ;
#77530=DIRECTION ( 'NONE',  ( -0.3543493200069163240, 0.000000000000000000, -0.9351131265310288487 ) ) ;
#77531=CARTESIAN_POINT ( 'NONE',  ( -0.3281693992235219515, -6.740707523384212863, 4.000000000000000000 ) ) ;
#77532=VECTOR ( 'NONE', #43422, 1000.000000000000227 ) ;
#77533=CARTESIAN_POINT ( 'NONE',  ( 63.29974487139158867, -27.71228299555250274, 4.000000000000000000 ) ) ;
#77534=LINE ( 'NONE', #76823, #92189 ) ;
#77535=CARTESIAN_POINT ( 'NONE',  ( 34.60428828362104525, 22.19175015946030172, 4.000000000000000000 ) ) ;
#77536=DIRECTION ( 'NONE',  ( -0.6830127018922181881, 0.6830127018922202975, -0.2588190451025214056 ) ) ;
#77537=VERTEX_POINT ( 'NONE', #143540 ) ;
#77538=DIRECTION ( 'NONE',  ( -0.000000000000000000, -0.3543493200069152693, 0.9351131265310292928 ) ) ;
#77540=ORIENTED_EDGE ( 'NONE', *, *, #82299, .T. ) ;
#77542=ORIENTED_EDGE ( 'NONE', *, *, #50166, .F. ) ;
#77543=CARTESIAN_POINT ( 'NONE',  ( -5.999999999999953815, 13.55218569542903317, 5.000000000000000000 ) ) ;
#77545=ORIENTED_EDGE ( 'NONE', *, *, #121689, .T. ) ;
#77546=CARTESIAN_POINT ( 'NONE',  ( -36.29974487139159578, -27.71228299555231445, 4.000000000000000000 ) ) ;
#77549=CARTESIAN_POINT ( 'NONE',  ( 28.49999999999981171, 16.18958161055405753, -11.56426086740805204 ) ) ;
#77550=ORIENTED_EDGE ( 'NONE', *, *, #102084, .T. ) ;
#77551=DIRECTION ( 'NONE',  ( -0.7071067811865487940, 0.7071067811865463515, 0.000000000000000000 ) ) ;
#77552=EDGE_LOOP ( 'NONE', ( #85793, #137630, #84396, #105183 ) ) ;
#77553=LINE ( 'NONE', #97855, #9644 ) ;
#77554=ADVANCED_FACE ( 'NONE', ( #119615 ), #118926, .F. ) ;
#77556=ORIENTED_EDGE ( 'NONE', *, *, #65769, .F. ) ;
#77560=ADVANCED_FACE ( 'NONE', ( #131240 ), #55845, .F. ) ;
#77561=CARTESIAN_POINT ( 'NONE',  ( 2.999999999999978240, -8.731860332648835765, -2.120594902707531926 ) ) ;
#77562=ORIENTED_EDGE ( 'NONE', *, *, #134174, .T. ) ;
#77564=EDGE_CURVE ( 'NONE', #50064, #51894, #66016, .T. ) ;
#77565=ORIENTED_EDGE ( 'NONE', *, *, #54012, .F. ) ;
#77566=CARTESIAN_POINT ( 'NONE',  ( 21.29974487139158512, -27.71228299555221142, 4.000000000000000000 ) ) ;
#77568=CARTESIAN_POINT ( 'NONE',  ( -15.75860074219783513, 21.72499999999999432, 5.000000000000000000 ) ) ;
#77569=EDGE_CURVE ( 'NONE', #94043, #33680, #64554, .T. ) ;
#77570=CARTESIAN_POINT ( 'NONE',  ( 75.48921356237309510, -27.52281430457107803, 5.000000000000000000 ) ) ;
#77571=VECTOR ( 'NONE', #31687, 1000.000000000000000 ) ;
#77572=VERTEX_POINT ( 'NONE', #88468 ) ;
#77573=EDGE_CURVE ( 'NONE', #113402, #50766, #98602, .T. ) ;
#77574=LINE ( 'NONE', #121742, #120693 ) ;
#77575=CARTESIAN_POINT ( 'NONE',  ( -26.99999999999981171, 13.55218569542903495, 5.000000000000000000 ) ) ;
#77576=VERTEX_POINT ( 'NONE', #142832 ) ;
#77577=CARTESIAN_POINT ( 'NONE',  ( -34.53569095963128177, 22.21392809009763170, 4.239552123775272463 ) ) ;
#77578=DIRECTION ( 'NONE',  ( -0.7071067811865487940, 0.7071067811865463515, -0.000000000000000000 ) ) ;
#77579=ORIENTED_EDGE ( 'NONE', *, *, #112427, .T. ) ;
#77580=EDGE_CURVE ( 'NONE', #125243, #73980, #55120, .T. ) ;
#77581=PLANE ( 'NONE',  #9211 ) ;
#77582=ORIENTED_EDGE ( 'NONE', *, *, #36153, .F. ) ;
#77583=ORIENTED_EDGE ( 'NONE', *, *, #72275, .F. ) ;
#77584=EDGE_CURVE ( 'NONE', #7658, #124601, #21768, .T. ) ;
#77585=CARTESIAN_POINT ( 'NONE',  ( -9.461603553705650427, -9.740707523384173783, 17.74957260769608780 ) ) ;
#77586=CARTESIAN_POINT ( 'NONE',  ( 14.29289321881336150, -9.740707523384182664, 5.000000000000000000 ) ) ;
#77588=CARTESIAN_POINT ( 'NONE',  ( -31.49999999999976552, -1.912538124160739095, 4.000000000000000000 ) ) ;
#77589=EDGE_CURVE ( 'NONE', #24379, #107684, #89174, .T. ) ;
#77590=LINE ( 'NONE', #111625, #128503 ) ;
#77591=VECTOR ( 'NONE', #17168, 1000.000000000000000 ) ;
#77592=LINE ( 'NONE', #57995, #18347 ) ;
#77593=FACE_OUTER_BOUND ( 'NONE', #21937, .T. ) ;
#77595=DIRECTION ( 'NONE',  ( -0.000000000000000000, -0.3543493200069152693, 0.9351131265310292928 ) ) ;
#77596=CARTESIAN_POINT ( 'NONE',  ( -34.49999999999975842, 3.431123077392154830, 4.000000000000000000 ) ) ;
#77597=PLANE ( 'NONE',  #139789 ) ;
#77598=DIRECTION ( 'NONE',  ( -0.3543493200069163240, -0.000000000000000000, -0.9351131265310288487 ) ) ;
#77600=DIRECTION ( 'NONE',  ( -0.7071067811865486830, -0.7071067811865464625, -0.000000000000000000 ) ) ;
#77601=CARTESIAN_POINT ( 'NONE',  ( 11.99999999999991296, -5.527737879153178824, -7.983877177622400012 ) ) ;
#77602=LINE ( 'NONE', #111638, #104379 ) ;
#77604=ORIENTED_EDGE ( 'NONE', *, *, #130696, .F. ) ;
#77605=ORIENTED_EDGE ( 'NONE', *, *, #83351, .F. ) ;
#77607=ORIENTED_EDGE ( 'NONE', *, *, #36775, .F. ) ;
#77609=ORIENTED_EDGE ( 'NONE', *, *, #97733, .F. ) ;
#77611=EDGE_CURVE ( 'NONE', #7821, #130956, #124643, .T. ) ;
#77616=LINE ( 'NONE', #121786, #134451 ) ;
#77618=CARTESIAN_POINT ( 'NONE',  ( 38.99451991528749062, 28.92564299267965211, 4.000000000000000000 ) ) ;
#77620=DIRECTION ( 'NONE',  ( 0.7071067811865487940, 0.7071067811865463515, 0.000000000000000000 ) ) ;
#77621=DIRECTION ( 'NONE',  ( 0.6830127018922181881, 0.6830127018922202975, -0.2588190451025214056 ) ) ;
#77622=CARTESIAN_POINT ( 'NONE',  ( -34.75611968250422024, 16.70565069852389328, 4.955485411084898928 ) ) ;
#77623=CARTESIAN_POINT ( 'NONE',  ( 34.92499999999998295, 22.22500000000000142, 4.000000000000000000 ) ) ;
#77624=DIRECTION ( 'NONE',  ( 0.7071067811865487940, 0.7071067811865463515, -0.000000000000000000 ) ) ;
#77626=EDGE_CURVE ( 'NONE', #44075, #88739, #114467, .T. ) ;
#77627=VECTOR ( 'NONE', #130572, 1000.000000000000227 ) ;
#77628=LINE ( 'NONE', #121098, #97772 ) ;
#77632=VECTOR ( 'NONE', #133170, 1000.000000000000000 ) ;
#77634=VERTEX_POINT ( 'NONE', #26056 ) ;
#77635=VECTOR ( 'NONE', #83598, 1000.000000000000000 ) ;
#77636=VECTOR ( 'NONE', #126793, 1000.000000000000227 ) ;
#77637=EDGE_CURVE ( 'NONE', #133910, #47388, #14458, .T. ) ;
#77638=LINE ( 'NONE', #100087, #31691 ) ;
#77640=DIRECTION ( 'NONE',  ( -0.7071067811865486830, 0.7071067811865464625, 0.000000000000000000 ) ) ;
#77641=CARTESIAN_POINT ( 'NONE',  ( 34.92499999999998295, -22.22500000000000142, 4.500000000000000888 ) ) ;
#77643=VERTEX_POINT ( 'NONE', #101457 ) ;
#77644=EDGE_CURVE ( 'NONE', #56258, #6222, #57283, .T. ) ;
#77645=ORIENTED_EDGE ( 'NONE', *, *, #102443, .T. ) ;
#77646=DIRECTION ( 'NONE',  ( 0.7071067811865487940, -0.7071067811865463515, 0.000000000000000000 ) ) ;
#77648=ORIENTED_EDGE ( 'NONE', *, *, #87936, .F. ) ;
#77649=VERTEX_POINT ( 'NONE', #102906 ) ;
#77652=ORIENTED_EDGE ( 'NONE', *, *, #46958, .T. ) ;
#77653=PLANE ( 'NONE',  #9751 ) ;
#77654=LINE ( 'NONE', #110937, #33942 ) ;
#77657=ORIENTED_EDGE ( 'NONE', *, *, #115857, .T. ) ;
#77658=CARTESIAN_POINT ( 'NONE',  ( -28.88982677111770059, -22.22500000000000853, 4.785647885939353863 ) ) ;
#77659=VERTEX_POINT ( 'NONE', #58737 ) ;
#77660=ORIENTED_EDGE ( 'NONE', *, *, #36437, .T. ) ;
#77661=ORIENTED_EDGE ( 'NONE', *, *, #58646, .T. ) ;
#77663=DIRECTION ( 'NONE',  ( -0.7071067811865486830, -0.7071067811865464625, -0.000000000000000000 ) ) ;
#77664=ADVANCED_FACE ( 'NONE', ( #134845 ), #113038, .T. ) ;
#77665=ORIENTED_EDGE ( 'NONE', *, *, #10425, .F. ) ;
#77666=LINE ( 'NONE', #120392, #11199 ) ;
#77667=DIRECTION ( 'NONE',  ( 0.7071067811865486830, -0.7071067811865464625, -0.000000000000000000 ) ) ;
#77669=CARTESIAN_POINT ( 'NONE',  ( -0.7071067811865398012, 5.259292476615665457, 5.000000000000000000 ) ) ;
#77671=FACE_BOUND ( 'NONE', #109846, .T. ) ;
#77672=VERTEX_POINT ( 'NONE', #25318 ) ;
#77673=LINE ( 'NONE', #45773, #31820 ) ;
#77674=PLANE ( 'NONE',  #139375 ) ;
#77675=DIRECTION ( 'NONE',  ( -0.7071067811865486830, 0.7071067811865464625, 0.000000000000000000 ) ) ;
#77677=EDGE_LOOP ( 'NONE', ( #103739, #89411, #65819, #84928 ) ) ;
#77678=CARTESIAN_POINT ( 'NONE',  ( 26.70025512860841488, -27.71228299555187391, 4.000000000000000000 ) ) ;
#77679=ORIENTED_EDGE ( 'NONE', *, *, #26607, .T. ) ;
#77680=ORIENTED_EDGE ( 'NONE', *, *, #97081, .T. ) ;
#77681=CARTESIAN_POINT ( 'NONE',  ( -3.328169399223503966, -18.74070752338408852, 4.000000000000000000 ) ) ;
#77682=ORIENTED_EDGE ( 'NONE', *, *, #30816, .F. ) ;
#77683=VECTOR ( 'NONE', #127168, 1000.000000000000000 ) ;
#77685=ORIENTED_EDGE ( 'NONE', *, *, #57566, .F. ) ;
#77686=DIRECTION ( 'NONE',  ( 0.6830127018922180770, -0.6830127018922204085, -0.2588190451025213501 ) ) ;
#77688=CARTESIAN_POINT ( 'NONE',  ( 33.48921356237309510, -27.52281430457078670, 5.000000000000000000 ) ) ;
#77689=ORIENTED_EDGE ( 'NONE', *, *, #58023, .T. ) ;
#77692=EDGE_CURVE ( 'NONE', #106843, #112433, #35540, .T. ) ;
#77693=VECTOR ( 'NONE', #83857, 1000.000000000000114 ) ;
#77694=CARTESIAN_POINT ( 'NONE',  ( 8.999999999999937828, -13.97847968911259464, -0.1324546996126583220 ) ) ;
#77695=CARTESIAN_POINT ( 'NONE',  ( 33.18398860626899705, 28.73617430169810305, 5.000000000000000000 ) ) ;
#77696=CARTESIAN_POINT ( 'NONE',  ( 0.000000000000000000, 0.000000000000000000, 5.000000000000000000 ) ) ;
#77697=CARTESIAN_POINT ( 'NONE',  ( 44.99451991528749772, 28.92564299267969474, 4.000000000000000000 ) ) ;
#77698=EDGE_LOOP ( 'NONE', ( #53107, #106195, #3104, #90788, #60899 ) ) ;
#77699=VERTEX_POINT ( 'NONE', #123952 ) ;
#77700=ORIENTED_EDGE ( 'NONE', *, *, #86390, .T. ) ;
#77701=CARTESIAN_POINT ( 'NONE',  ( 5.816011393731002066, 28.73617430169783304, 5.000000000000000000 ) ) ;
#77702=DIRECTION ( 'NONE',  ( 0.6830127018922181881, 0.6830127018922202975, -0.2588190451025214056 ) ) ;
#77703=ORIENTED_EDGE ( 'NONE', *, *, #33126, .F. ) ;
#77705=LINE ( 'NONE', #24029, #42008 ) ;
#77707=CARTESIAN_POINT ( 'NONE',  ( 39.29974487139159578, -27.71228299555233576, 4.000000000000000000 ) ) ;
#77708=VERTEX_POINT ( 'NONE', #102196 ) ;
#77709=CARTESIAN_POINT ( 'NONE',  ( 78.48921356237309510, -27.52281430457109934, 5.000000000000000000 ) ) ;
#77711=FACE_OUTER_BOUND ( 'NONE', #72120, .T. ) ;
#77714=EDGE_CURVE ( 'NONE', #117130, #17670, #3546, .T. ) ;
#77715=FACE_OUTER_BOUND ( 'NONE', #61944, .T. ) ;
#77716=ORIENTED_EDGE ( 'NONE', *, *, #42617, .T. ) ;
#77718=VECTOR ( 'NONE', #143097, 1000.000000000000000 ) ;
#77720=DIRECTION ( 'NONE',  ( -0.000000000000000000, -0.000000000000000000, 1.000000000000000000 ) ) ;
#77721=FACE_OUTER_BOUND ( 'NONE', #120850, .T. ) ;
#77722=CARTESIAN_POINT ( 'NONE',  ( -15.00548008471250228, 28.92564299267927552, 4.000000000000000000 ) ) ;
#77724=DIRECTION ( 'NONE',  ( -0.7071067811865486830, -0.7071067811865464625, -0.000000000000000000 ) ) ;
#77727=FACE_OUTER_BOUND ( 'NONE', #87368, .T. ) ;
#77728=DIRECTION ( 'NONE',  ( -0.7071067811865487940, 0.7071067811865463515, -0.000000000000000000 ) ) ;
#77729=ADVANCED_FACE ( 'NONE', ( #70147 ), #112191, .T. ) ;
#77730=EDGE_CURVE ( 'NONE', #43949, #27998, #136062, .T. ) ;
#77731=DIRECTION ( 'NONE',  ( 2.781805975412906507E-17, 0.3543493200069153248, 0.9351131265310292928 ) ) ;
#77732=ORIENTED_EDGE ( 'NONE', *, *, #46011, .F. ) ;
#77734=LINE ( 'NONE', #101599, #115922 ) ;
#77735=CARTESIAN_POINT ( 'NONE',  ( 19.05000000000000071, 3.174999999999997158, 5.000000000000000000 ) ) ;
#77736=ORIENTED_EDGE ( 'NONE', *, *, #131938, .F. ) ;
#77737=CARTESIAN_POINT ( 'NONE',  ( 31.49999999999977973, -15.29013452822851882, 0.3645803511611086511 ) ) ;
#77738=DIRECTION ( 'NONE',  ( -0.7071067811865487940, 0.7071067811865463515, -0.000000000000000000 ) ) ;
#77739=ORIENTED_EDGE ( 'NONE', *, *, #76655, .F. ) ;
#77740=EDGE_CURVE ( 'NONE', #86591, #24725, #91163, .T. ) ;
#77741=CARTESIAN_POINT ( 'NONE',  ( -34.92500000000001137, 21.72500000000000142, 5.000000000000000000 ) ) ;
#77743=ORIENTED_EDGE ( 'NONE', *, *, #143270, .T. ) ;
#77745=ORIENTED_EDGE ( 'NONE', *, *, #29923, .T. ) ;
#77747=EDGE_LOOP ( 'NONE', ( #124862, #20805, #130666, #15801 ) ) ;
#77749=EDGE_CURVE ( 'NONE', #61664, #45414, #100598, .T. ) ;
#77751=FACE_OUTER_BOUND ( 'NONE', #88407, .T. ) ;
#77752=LINE ( 'NONE', #4200, #79258 ) ;
#77753=VERTEX_POINT ( 'NONE', #58568 ) ;
#77754=FACE_OUTER_BOUND ( 'NONE', #1183, .T. ) ;
#77756=PLANE ( 'NONE',  #116486 ) ;
#77757=ADVANCED_FACE ( 'NONE', ( #22980 ), #57113, .F. ) ;
#77758=DIRECTION ( 'NONE',  ( -0.7071067811865487940, 0.7071067811865463515, -0.000000000000000000 ) ) ;
#77761=ORIENTED_EDGE ( 'NONE', *, *, #98984, .F. ) ;
#77762=ORIENTED_EDGE ( 'NONE', *, *, #122820, .T. ) ;
#77763=DIRECTION ( 'NONE',  ( 0.7071067811865487940, 0.7071067811865463515, 0.000000000000000000 ) ) ;
#77764=VERTEX_POINT ( 'NONE', #67248 ) ;
#77765=EDGE_LOOP ( 'NONE', ( #48005, #71769, #26718, #17765 ) ) ;
#77766=EDGE_CURVE ( 'NONE', #22361, #120155, #90418, .T. ) ;
#77767=LINE ( 'NONE', #56037, #133538 ) ;
#77768=CARTESIAN_POINT ( 'NONE',  ( 23.29298673570678346, -21.74070752338406720, 4.999753212805222446 ) ) ;
#77769=ORIENTED_EDGE ( 'NONE', *, *, #54787, .F. ) ;
#77770=PLANE ( 'NONE',  #11443 ) ;
#77773=DIRECTION ( 'NONE',  ( -0.7071067811865486830, 0.7071067811865464625, 0.000000000000000000 ) ) ;
#77775=ORIENTED_EDGE ( 'NONE', *, *, #25610, .T. ) ;
#77776=EDGE_CURVE ( 'NONE', #73203, #88923, #1241, .T. ) ;
#77777=CARTESIAN_POINT ( 'NONE',  ( -34.49999999999976552, 7.464255608400418573, 4.994342998332163219 ) ) ;
#77778=DIRECTION ( 'NONE',  ( 0.6830127018922180770, -0.6830127018922204085, -0.2588190451025213501 ) ) ;
#77780=DIRECTION ( 'NONE',  ( -0.6830127018922181881, 0.6830127018922202975, -0.2588190451025214056 ) ) ;
#77781=DIRECTION ( 'NONE',  ( -0.000000000000000000, 0.3543493200069153248, 0.9351131265310292928 ) ) ;
#77782=DIRECTION ( 'NONE',  ( 1.000000000000000000, 0.000000000000000000, 0.000000000000000000 ) ) ;
#77784=EDGE_CURVE ( 'NONE', #121955, #22749, #35358, .T. ) ;
#77785=AXIS2_PLACEMENT_3D ( 'NONE', #71762, #135589, #49307 ) ;
#77786=LINE ( 'NONE', #121966, #90764 ) ;
#77787=CARTESIAN_POINT ( 'NONE',  ( -18.18398860626898994, 28.73617430169800002, 5.000000000000000000 ) ) ;
#77788=ORIENTED_EDGE ( 'NONE', *, *, #75952, .F. ) ;
#77791=AXIS2_PLACEMENT_3D ( 'NONE', #51795, #95268, #108981 ) ;
#77792=PLANE ( 'NONE',  #34457 ) ;
#77793=CARTESIAN_POINT ( 'NONE',  ( 31.17183060077625001, -17.24070752338410628, 4.000000000000000000 ) ) ;
#77794=ORIENTED_EDGE ( 'NONE', *, *, #32490, .T. ) ;
#77795=PLANE ( 'NONE',  #54847 ) ;
#77796=LINE ( 'NONE', #19116, #60841 ) ;
#77798=VECTOR ( 'NONE', #114125, 1000.000000000000000 ) ;
#77799=ORIENTED_EDGE ( 'NONE', *, *, #90005, .F. ) ;
#77801=VERTEX_POINT ( 'NONE', #123789 ) ;
#77802=ORIENTED_EDGE ( 'NONE', *, *, #71416, .T. ) ;
#77803=DIRECTION ( 'NONE',  ( -0.000000000000000000, 0.000000000000000000, 1.000000000000000000 ) ) ;
#77806=CARTESIAN_POINT ( 'NONE',  ( 21.70710678118638981, -15.74070752338412404, 5.000000000000000000 ) ) ;
#77807=ORIENTED_EDGE ( 'NONE', *, *, #10153, .T. ) ;
#77808=CARTESIAN_POINT ( 'NONE',  ( -4.499999999999967137, 3.052185695429136647, 5.000000000000000000 ) ) ;
#77809=ORIENTED_EDGE ( 'NONE', *, *, #131568, .F. ) ;
#77811=CARTESIAN_POINT ( 'NONE',  ( 0.000000000000000000, 0.000000000000000000, 5.000000000000000000 ) ) ;
#77813=CARTESIAN_POINT ( 'NONE',  ( -4.499999999999968914, -4.796895815301026822, -3.611700055028691292 ) ) ;
#77814=CARTESIAN_POINT ( 'NONE',  ( -66.48921356237309510, -27.52281430457101763, 5.000000000000000000 ) ) ;
#77815=VECTOR ( 'NONE', #103438, 1000.000000000000000 ) ;
#77816=VECTOR ( 'NONE', #61946, 999.9999999999998863 ) ;
#77817=ORIENTED_EDGE ( 'NONE', *, *, #124042, .F. ) ;
#77818=DIRECTION ( 'NONE',  ( -0.000000000000000000, 0.3543493200069153248, 0.9351131265310292928 ) ) ;
#77820=CARTESIAN_POINT ( 'NONE',  ( -25.01459476339044130, 2.945717840782780428, 4.000000000000000000 ) ) ;
#77821=DIRECTION ( 'NONE',  ( -0.000000000000000000, 0.3543493200069153248, 0.9351131265310291818 ) ) ;
#77822=CARTESIAN_POINT ( 'NONE',  ( 10.17183060077640100, 0.7592924766157104211, 4.000000000000000000 ) ) ;
#77823=EDGE_CURVE ( 'NONE', #137750, #53081, #125192, .T. ) ;
#77824=ORIENTED_EDGE ( 'NONE', *, *, #68805, .T. ) ;
#77825=AXIS2_PLACEMENT_3D ( 'NONE', #87742, #110884, #111639 ) ;
#77826=LINE ( 'NONE', #124889, #86321 ) ;
#77828=ORIENTED_EDGE ( 'NONE', *, *, #55397, .T. ) ;
#77829=DIRECTION ( 'NONE',  ( -0.7071067811865486830, -0.7071067811865464625, -0.000000000000000000 ) ) ;
#77830=ORIENTED_EDGE ( 'NONE', *, *, #21916, .T. ) ;
#77831=CARTESIAN_POINT ( 'NONE',  ( 66.48921356237309510, -27.52281430457101763, 5.000000000000000000 ) ) ;
#77832=DIRECTION ( 'NONE',  ( -0.000000000000000000, 0.000000000000000000, 1.000000000000000000 ) ) ;
#77833=CARTESIAN_POINT ( 'NONE',  ( 39.48921356237310221, -27.52281430457082934, 5.000000000000000000 ) ) ;
#77834=ADVANCED_FACE ( 'NONE', ( #85780 ), #141608, .F. ) ;
#77835=FACE_BOUND ( 'NONE', #9189, .T. ) ;
#77836=DIRECTION ( 'NONE',  ( 0.7071067811865486830, -0.7071067811865464625, -0.000000000000000000 ) ) ;
#77837=FACE_OUTER_BOUND ( 'NONE', #52001, .T. ) ;
#77838=EDGE_CURVE ( 'NONE', #6035, #28590, #57260, .T. ) ;
#77841=VERTEX_POINT ( 'NONE', #130010 ) ;
#77843=EDGE_LOOP ( 'NONE', ( #90724, #64210, #21519, #109960 ) ) ;
#77844=ORIENTED_EDGE ( 'NONE', *, *, #60045, .T. ) ;
#77848=EDGE_CURVE ( 'NONE', #32886, #116795, #61415, .T. ) ;
#77850=EDGE_LOOP ( 'NONE', ( #53813, #45568, #4907, #98447 ) ) ;
#77851=PLANE ( 'NONE',  #106877 ) ;
#77852=VECTOR ( 'NONE', #44838, 1000.000000000000000 ) ;
#77854=DIRECTION ( 'NONE',  ( 0.7071067811865486830, -0.7071067811865464625, -0.000000000000000000 ) ) ;
#77855=CARTESIAN_POINT ( 'NONE',  ( -21.29974487139158512, -27.71228299555221142, 4.000000000000000000 ) ) ;
#77856=CARTESIAN_POINT ( 'NONE',  ( 69.48921356237309510, -27.52281430457103895, 5.000000000000000000 ) ) ;
#77857=DIRECTION ( 'NONE',  ( 0.7071067811865487940, -0.7071067811865463515, 0.000000000000000000 ) ) ;
#77858=PLANE ( 'NONE',  #114445 ) ;
#77859=FACE_OUTER_BOUND ( 'NONE', #115142, .T. ) ;
#77860=CARTESIAN_POINT ( 'NONE',  ( 15.48921356237309510, -27.52281430457066236, 5.000000000000000000 ) ) ;
#77861=ORIENTED_EDGE ( 'NONE', *, *, #74587, .T. ) ;
#77863=ADVANCED_FACE ( 'NONE', ( #72293 ), #140860, .F. ) ;
#77866=VERTEX_POINT ( 'NONE', #116457 ) ;
#77867=CARTESIAN_POINT ( 'NONE',  ( 57.18398860626899705, 28.73617430169827358, 5.000000000000000000 ) ) ;
#77868=CARTESIAN_POINT ( 'NONE',  ( -33.70710678118630454, -18.74070752338409562, 5.000000000000000000 ) ) ;
#77869=ORIENTED_EDGE ( 'NONE', *, *, #60669, .T. ) ;
#77870=VERTEX_POINT ( 'NONE', #27287 ) ;
#77872=CARTESIAN_POINT ( 'NONE',  ( 69.18398860626899705, 28.73617430169835529, 5.000000000000000000 ) ) ;
#77873=VERTEX_POINT ( 'NONE', #4062 ) ;
#77875=AXIS2_PLACEMENT_3D ( 'NONE', #60590, #138114, #136671 ) ;
#77876=CARTESIAN_POINT ( 'NONE',  ( -57.18398860626899705, 28.73617430169827358, 5.000000000000000000 ) ) ;
#77879=ORIENTED_EDGE ( 'NONE', *, *, #45037, .T. ) ;
#77880=VECTOR ( 'NONE', #137561, 1000.000000000000227 ) ;
#77881=FACE_OUTER_BOUND ( 'NONE', #119109, .T. ) ;
#77882=EDGE_CURVE ( 'NONE', #138848, #16402, #104861, .T. ) ;
#77883=DIRECTION ( 'NONE',  ( -0.6830127018922181881, 0.6830127018922202975, -0.2588190451025214056 ) ) ;
#77884=CARTESIAN_POINT ( 'NONE',  ( -3.183988606268992161, 28.73617430169789699, 5.000000000000000000 ) ) ;
#77885=DIRECTION ( 'NONE',  ( -0.000000000000000000, 0.000000000000000000, 1.000000000000000000 ) ) ;
#77886=ORIENTED_EDGE ( 'NONE', *, *, #44212, .F. ) ;
#77887=ORIENTED_EDGE ( 'NONE', *, *, #23922, .T. ) ;
#77889=ADVANCED_FACE ( 'NONE', ( #30719 ), #70837, .F. ) ;
#77891=CARTESIAN_POINT ( 'NONE',  ( -9.707013264292978505, -21.74070752338405654, 4.999753212805220670 ) ) ;
#77892=EDGE_LOOP ( 'NONE', ( #80148, #123980, #109783, #40435 ) ) ;
#77893=LINE ( 'NONE', #67015, #78209 ) ;
#77894=CARTESIAN_POINT ( 'NONE',  ( 15.18398860626900237, 28.73617430169797871, 5.000000000000000000 ) ) ;
#77895=EDGE_LOOP ( 'NONE', ( #132072, #44030, #83934, #67915 ) ) ;
#77896=VECTOR ( 'NONE', #429, 1000.000000000000227 ) ;
#77897=DIRECTION ( 'NONE',  ( 0.7071067811865486830, -0.7071067811865464625, -0.000000000000000000 ) ) ;
#77898=DIRECTION ( 'NONE',  ( 0.7071067811865487940, 0.7071067811865463515, 0.000000000000000000 ) ) ;
#77901=EDGE_CURVE ( 'NONE', #131775, #73925, #83122, .T. ) ;
#77902=CARTESIAN_POINT ( 'NONE',  ( -36.48921356237310221, -27.52281430457080802, 5.000000000000000000 ) ) ;
#77903=DIRECTION ( 'NONE',  ( 0.7071067811865487940, -0.7071067811865463515, 0.000000000000000000 ) ) ;
#77904=CARTESIAN_POINT ( 'NONE',  ( -36.13499573751600735, 3.759292476615678336, 15.36553568819734572 ) ) ;
#77906=EDGE_CURVE ( 'NONE', #87440, #82359, #122688, .T. ) ;
#77907=DIRECTION ( 'NONE',  ( 0.3543493200069162685, -0.000000000000000000, -0.9351131265310288487 ) ) ;
#77908=ORIENTED_EDGE ( 'NONE', *, *, #139333, .T. ) ;
#77909=ADVANCED_FACE ( 'NONE', ( #33582 ), #10351, .F. ) ;
#77910=DIRECTION ( 'NONE',  ( 0.7071067811865486830, -0.7071067811865464625, -0.000000000000000000 ) ) ;
#77911=ORIENTED_EDGE ( 'NONE', *, *, #79276, .T. ) ;
#77912=DIRECTION ( 'NONE',  ( 0.7071067811865487940, 0.7071067811865463515, -0.000000000000000000 ) ) ;
#77913=DIRECTION ( 'NONE',  ( -0.000000000000000000, -0.3543493200069152693, 0.9351131265310292928 ) ) ;
#77914=AXIS2_PLACEMENT_3D ( 'NONE', #27866, #104711, #5378 ) ;
#77915=AXIS2_PLACEMENT_3D ( 'NONE', #81581, #69265, #80154 ) ;
#77916=LINE ( 'NONE', #11172, #3471 ) ;
#77917=CARTESIAN_POINT ( 'NONE',  ( 20.29289321881331887, 20.25929247661551713, 5.000000000000000000 ) ) ;
#77918=VECTOR ( 'NONE', #74061, 999.9999999999998863 ) ;
#77919=EDGE_CURVE ( 'NONE', #109689, #94724, #54605, .T. ) ;
#77920=ORIENTED_EDGE ( 'NONE', *, *, #70884, .T. ) ;
#77921=LINE ( 'NONE', #113370, #18334 ) ;
#77922=CARTESIAN_POINT ( 'NONE',  ( 2.602085213965210642E-15, 19.55218569542897100, 5.000000000000000000 ) ) ;
#77923=EDGE_CURVE ( 'NONE', #143372, #7797, #12499, .T. ) ;
#77924=DIRECTION ( 'NONE',  ( -0.7071067811865487940, 0.7071067811865463515, 0.000000000000000000 ) ) ;
#77925=ORIENTED_EDGE ( 'NONE', *, *, #20982, .T. ) ;
#77926=CARTESIAN_POINT ( 'NONE',  ( -31.49999999999977973, 6.277155672890242677, -3.510561720658869067 ) ) ;
#77927=DIRECTION ( 'NONE',  ( 0.7071067811865487940, 0.7071067811865463515, 0.000000000000000000 ) ) ;
#77932=EDGE_CURVE ( 'NONE', #50763, #131707, #119812, .T. ) ;
#77934=PLANE ( 'NONE',  #132157 ) ;
#77937=CARTESIAN_POINT ( 'NONE',  ( 18.29974487139159223, -27.71228299555219010, 4.000000000000000000 ) ) ;
#77940=LINE ( 'NONE', #97522, #13054 ) ;
#77941=PLANE ( 'NONE',  #8333 ) ;
#77942=CARTESIAN_POINT ( 'NONE',  ( 20.81601139373100295, 28.73617430169773002, 5.000000000000000000 ) ) ;
#77943=DIRECTION ( 'NONE',  ( -0.7071067811865486830, -0.7071067811865464625, 0.000000000000000000 ) ) ;
#77944=FACE_OUTER_BOUND ( 'NONE', #54264, .T. ) ;
#77945=DIRECTION ( 'NONE',  ( -0.000000000000000000, 0.000000000000000000, 1.000000000000000000 ) ) ;
#77946=ORIENTED_EDGE ( 'NONE', *, *, #90825, .F. ) ;
#77947=ORIENTED_EDGE ( 'NONE', *, *, #100564, .T. ) ;
#77948=DIRECTION ( 'NONE',  ( -0.6830127018922180770, -0.6830127018922204085, -0.2588190451025213501 ) ) ;
#77951=EDGE_CURVE ( 'NONE', #31681, #119020, #143026, .T. ) ;
#77952=CARTESIAN_POINT ( 'NONE',  ( -22.49999999999984368, -8.568876922607728375, 4.000000000000000000 ) ) ;
#77956=FACE_OUTER_BOUND ( 'NONE', #107386, .T. ) ;
#77957=EDGE_CURVE ( 'NONE', #116108, #81904, #894, .T. ) ;
#77960=ORIENTED_EDGE ( 'NONE', *, *, #138817, .F. ) ;
#77962=DIRECTION ( 'NONE',  ( 1.000000000000000000, 0.000000000000000000, 0.000000000000000000 ) ) ;
#77963=DIRECTION ( 'NONE',  ( -0.7071067811865487940, 0.7071067811865463515, 0.000000000000000000 ) ) ;
#77964=CARTESIAN_POINT ( 'NONE',  ( 69.18398860626899705, 28.73617430169835529, 5.000000000000000000 ) ) ;
#77965=VECTOR ( 'NONE', #36260, 1000.000000000000227 ) ;
#77966=VERTEX_POINT ( 'NONE', #56054 ) ;
#77967=ADVANCED_FACE ( 'NONE', ( #53907 ), #45182, .F. ) ;
#77970=ORIENTED_EDGE ( 'NONE', *, *, #54584, .F. ) ;
#77971=DIRECTION ( 'NONE',  ( -0.000000000000000000, 0.000000000000000000, 1.000000000000000000 ) ) ;
#77973=LINE ( 'NONE', #22821, #6087 ) ;
#77974=AXIS2_PLACEMENT_3D ( 'NONE', #82763, #4401, #92908 ) ;
#77976=CARTESIAN_POINT ( 'NONE',  ( 17.29289321881333308, -3.740707523384244837, 5.000000000000000000 ) ) ;
#77978=CARTESIAN_POINT ( 'NONE',  ( -7.499999999999951150, 13.56627193232214523, -10.57019076586070483 ) ) ;
#77979=DIRECTION ( 'NONE',  ( -0.000000000000000000, 0.3543493200069153248, 0.9351131265310292928 ) ) ;
#77980=VECTOR ( 'NONE', #106495, 1000.000000000000000 ) ;
#77982=CARTESIAN_POINT ( 'NONE',  ( -30.70710678118632231, -15.74070752338412760, 5.000000000000000000 ) ) ;
#77984=ORIENTED_EDGE ( 'NONE', *, *, #62543, .T. ) ;
#77985=DIRECTION ( 'NONE',  ( 0.7071067811865487940, 0.7071067811865463515, 0.000000000000000000 ) ) ;
#77986=DIRECTION ( 'NONE',  ( 0.7071067811865487940, 0.7071067811865463515, 0.000000000000000000 ) ) ;
#77988=CARTESIAN_POINT ( 'NONE',  ( -23.70025512860841133, -27.71228299555189523, 4.000000000000000000 ) ) ;
#77991=ORIENTED_EDGE ( 'NONE', *, *, #82369, .T. ) ;
#77993=VERTEX_POINT ( 'NONE', #89358 ) ;
#77994=VECTOR ( 'NONE', #91045, 999.9999999999998863 ) ;
#77996=DIRECTION ( 'NONE',  ( 0.7071067811865487940, 0.7071067811865463515, -0.000000000000000000 ) ) ;
#77997=CARTESIAN_POINT ( 'NONE',  ( -31.82816939922330945, -8.240707523384191546, 4.000000000000000000 ) ) ;
#77998=LINE ( 'NONE', #68560, #75779 ) ;
#78002=ORIENTED_EDGE ( 'NONE', *, *, #58024, .T. ) ;
#78003=ORIENTED_EDGE ( 'NONE', *, *, #81944, .F. ) ;
#78006=ORIENTED_EDGE ( 'NONE', *, *, #44034, .T. ) ;
#78009=DIRECTION ( 'NONE',  ( -0.7071067811865486830, -0.7071067811865464625, -0.000000000000000000 ) ) ;
#78010=ORIENTED_EDGE ( 'NONE', *, *, #70993, .F. ) ;
#78012=VECTOR ( 'NONE', #63578, 1000.000000000000227 ) ;
#78014=FACE_BOUND ( 'NONE', #127764, .T. ) ;
#78016=DIRECTION ( 'NONE',  ( -0.7071067811865487940, 0.7071067811865463515, 0.000000000000000000 ) ) ;
#78017=LINE ( 'NONE', #44714, #8802 ) ;
#78018=CARTESIAN_POINT ( 'NONE',  ( 31.60343192894623954, -14.24070752338412582, 19.24067776001733066 ) ) ;
#78019=VECTOR ( 'NONE', #10219, 1000.000000000000000 ) ;
#78020=VECTOR ( 'NONE', #110236, 1000.000000000000000 ) ;
#78022=ADVANCED_FACE ( 'NONE', ( #120517 ), #121962, .F. ) ;
#78023=LINE ( 'NONE', #135272, #78987 ) ;
#78026=VECTOR ( 'NONE', #16409, 1000.000000000000000 ) ;
#78027=ORIENTED_EDGE ( 'NONE', *, *, #56957, .F. ) ;
#78029=VERTEX_POINT ( 'NONE', #76350 ) ;
#78030=ADVANCED_FACE ( 'NONE', ( #132898 ), #78491, .F. ) ;
#78031=FACE_OUTER_BOUND ( 'NONE', #43438, .T. ) ;
#78033=VECTOR ( 'NONE', #24470, 999.9999999999998863 ) ;
#78034=VECTOR ( 'NONE', #40721, 1000.000000000000000 ) ;
#78036=CARTESIAN_POINT ( 'NONE',  ( 6.758600742197917732, 21.72500000000000142, 5.000000000000000000 ) ) ;
#78037=EDGE_CURVE ( 'NONE', #24063, #111037, #100939, .T. ) ;
#78038=PLANE ( 'NONE',  #33261 ) ;
#78039=ORIENTED_EDGE ( 'NONE', *, *, #9165, .T. ) ;
#78041=DIRECTION ( 'NONE',  ( -0.7071067811865486830, 0.7071067811865464625, 0.000000000000000000 ) ) ;
#78042=CARTESIAN_POINT ( 'NONE',  ( -12.18398860626900060, 28.73617430169795739, 5.000000000000000000 ) ) ;
#78043=DIRECTION ( 'NONE',  ( -0.3543493200069162685, -0.000000000000000000, -0.9351131265310288487 ) ) ;
#78044=PLANE ( 'NONE',  #50416 ) ;
#78045=EDGE_CURVE ( 'NONE', #33966, #115267, #72089, .T. ) ;
#78046=DIRECTION ( 'NONE',  ( 0.7071067811865487940, 0.7071067811865463515, -0.000000000000000000 ) ) ;
#78047=VERTEX_POINT ( 'NONE', #87221 ) ;
#78048=CARTESIAN_POINT ( 'NONE',  ( -0.1839886062690032631, 28.73617430169787568, 5.000000000000000000 ) ) ;
#78049=CARTESIAN_POINT ( 'NONE',  ( 8.671830600776413434, -6.740707523384218192, 4.000000000000000000 ) ) ;
#78050=ORIENTED_EDGE ( 'NONE', *, *, #135406, .F. ) ;
#78052=ORIENTED_EDGE ( 'NONE', *, *, #19935, .T. ) ;
#78054=VECTOR ( 'NONE', #80218, 1000.000000000000000 ) ;
#78055=EDGE_CURVE ( 'NONE', #49512, #31384, #5167, .T. ) ;
#78056=ORIENTED_EDGE ( 'NONE', *, *, #92520, .T. ) ;
#78058=VECTOR ( 'NONE', #123658, 1000.000000000000000 ) ;
#78059=FACE_OUTER_BOUND ( 'NONE', #71124, .T. ) ;
#78061=CARTESIAN_POINT ( 'NONE',  ( -14.20710678118644665, 6.759292476615649470, 5.000000000000000000 ) ) ;
#78062=EDGE_CURVE ( 'NONE', #88361, #141224, #48022, .T. ) ;
#78063=EDGE_LOOP ( 'NONE', ( #18856, #74168, #76250 ) ) ;
#78064=DIRECTION ( 'NONE',  ( 0.7071067811865487940, -0.7071067811865463515, 0.000000000000000000 ) ) ;
#78065=VECTOR ( 'NONE', #11427, 1000.000000000000227 ) ;
#78067=VERTEX_POINT ( 'NONE', #79248 ) ;
#78068=CARTESIAN_POINT ( 'NONE',  ( -34.92500000000001137, 21.72500000000000142, 0.4999999999999995559 ) ) ;
#78069=LINE ( 'NONE', #9928, #128525 ) ;
#78071=ORIENTED_EDGE ( 'NONE', *, *, #50584, .F. ) ;
#78072=FACE_OUTER_BOUND ( 'NONE', #752, .T. ) ;
#78073=VERTEX_POINT ( 'NONE', #37859 ) ;
#78074=EDGE_CURVE ( 'NONE', #99199, #53035, #112537, .T. ) ;
#78075=EDGE_LOOP ( 'NONE', ( #76879, #33146, #44007, #122056 ) ) ;
#78076=ORIENTED_EDGE ( 'NONE', *, *, #132025, .T. ) ;
#78078=VECTOR ( 'NONE', #6387, 1000.000000000000000 ) ;
#78079=ADVANCED_FACE ( 'NONE', ( #135045 ), #68364, .T. ) ;
#78080=FACE_OUTER_BOUND ( 'NONE', #43086, .T. ) ;
#78081=CARTESIAN_POINT ( 'NONE',  ( 25.49999999999982947, 6.052185695429106893, 5.000000000000000000 ) ) ;
#78082=PLANE ( 'NONE',  #141483 ) ;
#78083=ORIENTED_EDGE ( 'NONE', *, *, #9914, .T. ) ;
#78085=CARTESIAN_POINT ( 'NONE',  ( -34.92500000000001137, 22.22500000000000142, 4.000000000000000000 ) ) ;
#78086=DIRECTION ( 'NONE',  ( -0.7071067811865486830, -0.7071067811865464625, 0.000000000000000000 ) ) ;
#78087=AXIS2_PLACEMENT_3D ( 'NONE', #19696, #131324, #65387 ) ;
#78088=EDGE_CURVE ( 'NONE', #100625, #140758, #125577, .T. ) ;
#78089=DIRECTION ( 'NONE',  ( -0.7071067811865487940, 0.7071067811865463515, 0.000000000000000000 ) ) ;
#78091=ORIENTED_EDGE ( 'NONE', *, *, #62369, .F. ) ;
#78092=ORIENTED_EDGE ( 'NONE', *, *, #52798, .T. ) ;
#78094=LINE ( 'NONE', #46202, #23211 ) ;
#78097=ADVANCED_FACE ( 'NONE', ( #137158 ), #70517, .F. ) ;
#78098=CARTESIAN_POINT ( 'NONE',  ( -33.18398860626899705, 28.73617430169810305, 5.000000000000000000 ) ) ;
#78100=DIRECTION ( 'NONE',  ( -0.6830127018922180770, -0.6830127018922204085, -0.2588190451025213501 ) ) ;
#78102=CARTESIAN_POINT ( 'NONE',  ( 14.12514619309225772, -14.24070752338413648, 9.401115078912624767 ) ) ;
#78103=CARTESIAN_POINT ( 'NONE',  ( 5.207106781186514155, 18.75929247661552068, 5.000000000000000000 ) ) ;
#78104=VERTEX_POINT ( 'NONE', #135727 ) ;
#78106=ORIENTED_EDGE ( 'NONE', *, *, #92239, .T. ) ;
#78108=EDGE_LOOP ( 'NONE', ( #67717, #12826, #88521, #9816 ) ) ;
#78109=LINE ( 'NONE', #82395, #120097 ) ;
#78111=ORIENTED_EDGE ( 'NONE', *, *, #88611, .T. ) ;
#78112=VECTOR ( 'NONE', #15894, 999.9999999999998863 ) ;
#78113=CARTESIAN_POINT ( 'NONE',  ( -28.26506670282034150, 12.75929247661558286, 18.34774599283962360 ) ) ;
#78114=LINE ( 'NONE', #110689, #81998 ) ;
#78115=ORIENTED_EDGE ( 'NONE', *, *, #34613, .F. ) ;
#78117=ORIENTED_EDGE ( 'NONE', *, *, #36114, .T. ) ;
#78121=VECTOR ( 'NONE', #30020, 1000.000000000000000 ) ;
#78122=VECTOR ( 'NONE', #131859, 1000.000000000000000 ) ;
#78123=DIRECTION ( 'NONE',  ( -0.7071067811865487940, 0.7071067811865463515, -0.000000000000000000 ) ) ;
#78124=ADVANCED_FACE ( 'NONE', ( #26949 ), #124840, .T. ) ;
#78125=VECTOR ( 'NONE', #58041, 999.9999999999998863 ) ;
#78127=DIRECTION ( 'NONE',  ( -0.6830127018922180770, -0.6830127018922204085, -0.2588190451025213501 ) ) ;
#78130=PLANE ( 'NONE',  #93615 ) ;
#78131=DIRECTION ( 'NONE',  ( 0.7071067811865486830, -0.7071067811865464625, -0.000000000000000000 ) ) ;
#78133=DIRECTION ( 'NONE',  ( 0.7071067811865487940, 0.7071067811865463515, 0.000000000000000000 ) ) ;
#78134=AXIS2_PLACEMENT_3D ( 'NONE', #46279, #69441, #1280 ) ;
#78135=DIRECTION ( 'NONE',  ( 0.3543493200069162685, -0.000000000000000000, -0.9351131265310288487 ) ) ;
#78136=CARTESIAN_POINT ( 'NONE',  ( 15.18398860626900237, 28.73617430169797871, 5.000000000000000000 ) ) ;
#78137=EDGE_LOOP ( 'NONE', ( #62039, #7537, #70098, #107513, #63805 ) ) ;
#78138=ORIENTED_EDGE ( 'NONE', *, *, #128752, .T. ) ;
#78139=LINE ( 'NONE', #143371, #9654 ) ;
#78140=ORIENTED_EDGE ( 'NONE', *, *, #39705, .F. ) ;
#78142=PLANE ( 'NONE',  #6282 ) ;
#78143=DIRECTION ( 'NONE',  ( -0.7071067811865487940, 0.7071067811865463515, -0.000000000000000000 ) ) ;
#78144=FACE_OUTER_BOUND ( 'NONE', #59803, .T. ) ;
#78148=CARTESIAN_POINT ( 'NONE',  ( 6.981552653643259276, 18.75929247661552424, 20.33588619593441393 ) ) ;
#78149=PLANE ( 'NONE',  #99714 ) ;
#78150=CARTESIAN_POINT ( 'NONE',  ( 0.7816268829249468642, 21.74787736706806385, 4.999607392498049308 ) ) ;
#78151=CARTESIAN_POINT ( 'NONE',  ( 29.99999999999979039, 9.631307414974347836, -9.079085613539472632 ) ) ;
#78152=LINE ( 'NONE', #99888, #1161 ) ;
#78155=VECTOR ( 'NONE', #114753, 1000.000000000000000 ) ;
#78156=LINE ( 'NONE', #122331, #126331 ) ;
#78157=LINE ( 'NONE', #89727, #9942 ) ;
#78158=LINE ( 'NONE', #67281, #15468 ) ;
#78159=( BOUNDED_CURVE ( )  B_SPLINE_CURVE ( 3, ( #132316, #142460, #64181, #42452 ),
 .UNSPECIFIED., .F., .T. ) 
 B_SPLINE_CURVE_WITH_KNOTS ( ( 4, 4 ),
 ( 1.208578181583233491, 1.359146454359400957 ),
 .UNSPECIFIED. ) 
 CURVE ( )  GEOMETRIC_REPRESENTATION_ITEM ( )  RATIONAL_B_SPLINE_CURVE ( ( 1.000000000000000000, 0.9981116584018960847, 0.9981116584018960847, 1.000000000000000000 ) ) 
 REPRESENTATION_ITEM ( '' )  );
#78160=DIRECTION ( 'NONE',  ( 0.7071067811865487940, 0.7071067811865463515, 0.000000000000000000 ) ) ;
#78161=ORIENTED_EDGE ( 'NONE', *, *, #31862, .F. ) ;
#78162=ORIENTED_EDGE ( 'NONE', *, *, #121882, .F. ) ;
#78163=ORIENTED_EDGE ( 'NONE', *, *, #60517, .F. ) ;
#78165=VECTOR ( 'NONE', #117973, 999.9999999999998863 ) ;
#78166=ORIENTED_EDGE ( 'NONE', *, *, #62774, .F. ) ;
#78167=LINE ( 'NONE', #122343, #76386 ) ;
#78168=DIRECTION ( 'NONE',  ( -0.7071067811865487940, 0.7071067811865463515, -0.000000000000000000 ) ) ;
#78170=DIRECTION ( 'NONE',  ( -0.7071067811865486830, -0.7071067811865464625, 0.000000000000000000 ) ) ;
#78172=EDGE_LOOP ( 'NONE', ( #133226, #67650, #17852, #79975 ) ) ;
#78173=CARTESIAN_POINT ( 'NONE',  ( 12.18398860626900060, 28.73617430169795739, 5.000000000000000000 ) ) ;
#78174=FACE_OUTER_BOUND ( 'NONE', #92967, .T. ) ;
#78177=VERTEX_POINT ( 'NONE', #26254 ) ;
#78178=LINE ( 'NONE', #111500, #90657 ) ;
#78179=EDGE_CURVE ( 'NONE', #140110, #44742, #114660, .T. ) ;
#78182=ORIENTED_EDGE ( 'NONE', *, *, #111411, .F. ) ;
#78183=AXIS2_PLACEMENT_3D ( 'NONE', #99037, #21509, #132449 ) ;
#78184=FACE_OUTER_BOUND ( 'NONE', #137693, .T. ) ;
#78185=EDGE_CURVE ( 'NONE', #134257, #98588, #3051, .T. ) ;
#78186=EDGE_CURVE ( 'NONE', #138636, #77870, #101654, .T. ) ;
#78187=CARTESIAN_POINT ( 'NONE',  ( 36.29974487139159578, -27.71228299555231445, 4.000000000000000000 ) ) ;
#78189=DIRECTION ( 'NONE',  ( -0.7071067811865486830, -0.7071067811865464625, -0.000000000000000000 ) ) ;
#78190=EDGE_CURVE ( 'NONE', #130315, #46312, #113966, .T. ) ;
#78191=EDGE_CURVE ( 'NONE', #114924, #77276, #58213, .T. ) ;
#78192=CARTESIAN_POINT ( 'NONE',  ( 81.48921356237309510, -27.52281430457112066, 5.000000000000000000 ) ) ;
#78193=VERTEX_POINT ( 'NONE', #58934 ) ;
#78194=AXIS2_PLACEMENT_3D ( 'NONE', #72190, #127975, #83026 ) ;
#78195=VERTEX_POINT ( 'NONE', #91514 ) ;
#78196=FACE_OUTER_BOUND ( 'NONE', #54483, .T. ) ;
#78197=EDGE_CURVE ( 'NONE', #76630, #23935, #3732, .T. ) ;
#78198=ORIENTED_EDGE ( 'NONE', *, *, #107482, .T. ) ;
#78199=ORIENTED_EDGE ( 'NONE', *, *, #31210, .F. ) ;
#78200=ADVANCED_FACE ( 'NONE', ( #59616 ), #4413, .F. ) ;
#78201=EDGE_CURVE ( 'NONE', #136035, #83916, #105228, .T. ) ;
#78203=CARTESIAN_POINT ( 'NONE',  ( -66.18398860626901126, 28.73617430169833753, 5.000000000000000000 ) ) ;
#78204=ORIENTED_EDGE ( 'NONE', *, *, #95989, .F. ) ;
#78205=DIRECTION ( 'NONE',  ( 0.7071067811865487940, 0.7071067811865463515, 0.000000000000000000 ) ) ;
#78206=CARTESIAN_POINT ( 'NONE',  ( -9.489213562373095101, -27.52281430457062328, 5.000000000000000000 ) ) ;
#78207=FACE_OUTER_BOUND ( 'NONE', #18247, .T. ) ;
#78209=VECTOR ( 'NONE', #45294, 1000.000000000000000 ) ;
#78210=DIRECTION ( 'NONE',  ( 0.3543493200069162685, -0.000000000000000000, -0.9351131265310288487 ) ) ;
#78212=EDGE_CURVE ( 'NONE', #58576, #90134, #105916, .T. ) ;
#78215=CARTESIAN_POINT ( 'NONE',  ( -32.99999999999976552, -3.485240976185108863, -4.108735105802471921 ) ) ;
#78216=VERTEX_POINT ( 'NONE', #84229 ) ;
#78218=VERTEX_POINT ( 'NONE', #96457 ) ;
#78220=ORIENTED_EDGE ( 'NONE', *, *, #126661, .T. ) ;
#78221=ORIENTED_EDGE ( 'NONE', *, *, #105049, .T. ) ;
#78223=VECTOR ( 'NONE', #2015, 1000.000000000000000 ) ;
#78224=ORIENTED_EDGE ( 'NONE', *, *, #93430, .F. ) ;
#78225=VECTOR ( 'NONE', #100136, 999.9999999999998863 ) ;
#78226=CARTESIAN_POINT ( 'NONE',  ( -34.92500000000001137, 0.5846064065779844610, -3.200354092940483230 ) ) ;
#78227=LINE ( 'NONE', #24537, #99213 ) ;
#78228=DIRECTION ( 'NONE',  ( -0.6830127018922180770, -0.6830127018922204085, -0.2588190451025213501 ) ) ;
#78230=DIRECTION ( 'NONE',  ( 0.6830127018922181881, 0.6830127018922202975, -0.2588190451025214056 ) ) ;
#78231=CARTESIAN_POINT ( 'NONE',  ( 27.48921356237309155, -27.52281430457074762, 5.000000000000000000 ) ) ;
#78232=DIRECTION ( 'NONE',  ( -0.7071067811865486830, -0.7071067811865464625, 0.000000000000000000 ) ) ;
#78233=ADVANCED_FACE ( 'NONE', ( #50151 ), #94349, .F. ) ;
#78235=CARTESIAN_POINT ( 'NONE',  ( -7.499999999999940492, -20.94781430457061333, 5.000000000000000000 ) ) ;
#78236=ADVANCED_FACE ( 'NONE', ( #85601 ), #73338, .F. ) ;
#78238=DIRECTION ( 'NONE',  ( 0.7071067811865487940, 0.7071067811865463515, -0.000000000000000000 ) ) ;
#78239=CARTESIAN_POINT ( 'NONE',  ( -34.92500000000001137, -22.22500000000000142, 4.500000000000000888 ) ) ;
#78242=EDGE_CURVE ( 'NONE', #125874, #7538, #116095, .T. ) ;
#78243=ORIENTED_EDGE ( 'NONE', *, *, #129152, .T. ) ;
#78244=VERTEX_POINT ( 'NONE', #108050 ) ;
#78245=DIRECTION ( 'NONE',  ( 0.7071067811865487940, 0.7071067811865463515, -0.000000000000000000 ) ) ;
#78246=EDGE_LOOP ( 'NONE', ( #25781, #58346, #114442, #36829 ) ) ;
#78247=EDGE_CURVE ( 'NONE', #45102, #117033, #52970, .T. ) ;
#78248=EDGE_CURVE ( 'NONE', #119991, #34098, #29100, .T. ) ;
#78250=CARTESIAN_POINT ( 'NONE',  ( 31.49999999999978684, -7.420205493532869845, -2.617629953481181992 ) ) ;
#78252=CARTESIAN_POINT ( 'NONE',  ( -2.999999999999981792, 14.87792677143808362, -11.06722581663440508 ) ) ;
#78253=LINE ( 'NONE', #132659, #127433 ) ;
#78256=DIRECTION ( 'NONE',  ( -0.6830127018922181881, 0.6830127018922202975, -0.2588190451025214056 ) ) ;
#78257=ORIENTED_EDGE ( 'NONE', *, *, #84087, .T. ) ;
#78258=LINE ( 'NONE', #122440, #120894 ) ;
#78260=ORIENTED_EDGE ( 'NONE', *, *, #90309, .T. ) ;
#78262=LINE ( 'NONE', #107982, #25085 ) ;
#78265=ORIENTED_EDGE ( 'NONE', *, *, #5491, .F. ) ;
#78266=ORIENTED_EDGE ( 'NONE', *, *, #417, .F. ) ;
#78267=ORIENTED_EDGE ( 'NONE', *, *, #54144, .F. ) ;
#78269=DIRECTION ( 'NONE',  ( -1.000000000000000000, 0.000000000000000000, 0.000000000000000000 ) ) ;
#78270=DIRECTION ( 'NONE',  ( -0.000000000000000000, 0.3543493200069153248, 0.9351131265310292928 ) ) ;
#78271=CARTESIAN_POINT ( 'NONE',  ( 0.000000000000000000, 0.000000000000000000, 5.000000000000000000 ) ) ;
#78273=DIRECTION ( 'NONE',  ( -0.000000000000000000, -0.3543493200069152693, 0.9351131265310292928 ) ) ;
#78274=ADVANCED_FACE ( 'NONE', ( #51584 ), #95777, .F. ) ;
#78275=CARTESIAN_POINT ( 'NONE',  ( 13.17183060077637968, 0.7592924766157086447, 4.000000000000000000 ) ) ;
#78276=CARTESIAN_POINT ( 'NONE',  ( 23.99999999999983302, 7.931123077392101095, 4.000000000000000000 ) ) ;
#78277=VERTEX_POINT ( 'NONE', #140024 ) ;
#78279=CARTESIAN_POINT ( 'NONE',  ( -54.18398860626899705, 28.73617430169825226, 5.000000000000000000 ) ) ;
#78280=ORIENTED_EDGE ( 'NONE', *, *, #32609, .F. ) ;
#78282=ORIENTED_EDGE ( 'NONE', *, *, #141371, .F. ) ;
#78283=ADVANCED_FACE ( 'NONE', ( #39278 ), #83501, .F. ) ;
#78284=EDGE_LOOP ( 'NONE', ( #61093, #124728, #120497, #118939 ) ) ;
#78285=DIRECTION ( 'NONE',  ( -0.000000000000000000, 0.3543493200069153248, 0.9351131265310292928 ) ) ;
#78286=CARTESIAN_POINT ( 'NONE',  ( 51.48921356237309510, -27.52281430457091460, 5.000000000000000000 ) ) ;
#78287=ORIENTED_EDGE ( 'NONE', *, *, #20569, .F. ) ;
#78288=LINE ( 'NONE', #67427, #86049 ) ;
#78289=CARTESIAN_POINT ( 'NONE',  ( 34.49999999999975131, -1.592773361805337906, -6.492772025301308148 ) ) ;
#78291=CARTESIAN_POINT ( 'NONE',  ( -13.49999999999990408, 3.653845994658375673, -4.504631822206340175 ) ) ;
#78292=VECTOR ( 'NONE', #9720, 1000.000000000000000 ) ;
#78293=CARTESIAN_POINT ( 'NONE',  ( -4.499999999999968914, 12.43112307739206024, 4.000000000000000000 ) ) ;
#78294=CARTESIAN_POINT ( 'NONE',  ( -33.18398860626899705, 28.73617430169810305, 5.000000000000000000 ) ) ;
#78295=CARTESIAN_POINT ( 'NONE',  ( -16.49999999999986500, 19.08746187583904685, 4.000000000000000000 ) ) ;
#78296=CARTESIAN_POINT ( 'NONE',  ( 15.18398860626900237, 28.73617430169797871, 5.000000000000000000 ) ) ;
#78297=LINE ( 'NONE', #10162, #117731 ) ;
#78300=PLANE ( 'NONE',  #103758 ) ;
#78301=LINE ( 'NONE', #119620, #68626 ) ;
#78302=ORIENTED_EDGE ( 'NONE', *, *, #132591, .F. ) ;
#78303=ADVANCED_FACE ( 'NONE', ( #118223 ), #129118, .F. ) ;
#78304=EDGE_LOOP ( 'NONE', ( #103258, #63347, #133332, #105150 ) ) ;
#78306=EDGE_CURVE ( 'NONE', #56334, #134021, #29796, .T. ) ;
#78307=ORIENTED_EDGE ( 'NONE', *, *, #105650, .T. ) ;
#78308=ORIENTED_EDGE ( 'NONE', *, *, #134654, .T. ) ;
#78309=ORIENTED_EDGE ( 'NONE', *, *, #1232, .T. ) ;
#78310=LINE ( 'NONE', #89187, #124417 ) ;
#78311=CARTESIAN_POINT ( 'NONE',  ( -31.49999999999977263, 1.087461875839230707, 4.000000000000000000 ) ) ;
#78313=VECTOR ( 'NONE', #25634, 1000.000000000000000 ) ;
#78314=CARTESIAN_POINT ( 'NONE',  ( -28.49999999999979750, -13.53360074219760101, 5.000000000000000000 ) ) ;
#78315=PLANE ( 'NONE',  #51140 ) ;
#78317=DIRECTION ( 'NONE',  ( -0.7071067811865486830, -0.7071067811865464625, 0.000000000000000000 ) ) ;
#78318=ORIENTED_EDGE ( 'NONE', *, *, #116781, .F. ) ;
#78319=ADVANCED_FACE ( 'NONE', ( #18930 ), #41393, .F. ) ;
#78320=CARTESIAN_POINT ( 'NONE',  ( 19.42650926608378725, -2.782569431601979559, 4.369986656771211564 ) ) ;
#78322=CARTESIAN_POINT ( 'NONE',  ( 14.99999999999989519, -15.03360074219758857, 5.000000000000000000 ) ) ;
#78324=LINE ( 'NONE', #134871, #59124 ) ;
#78325=PLANE ( 'NONE',  #70134 ) ;
#78326=DIRECTION ( 'NONE',  ( 0.7071067811865487940, 0.7071067811865463515, 0.000000000000000000 ) ) ;
#78327=VECTOR ( 'NONE', #4135, 999.9999999999998863 ) ;
#78330=VERTEX_POINT ( 'NONE', #19644 ) ;
#78331=VERTEX_POINT ( 'NONE', #31956 ) ;
#78335=CARTESIAN_POINT ( 'NONE',  ( 3.183988606268992161, 28.73617430169789699, 5.000000000000000000 ) ) ;
#78336=DIRECTION ( 'NONE',  ( 0.7071067811865487940, 0.7071067811865463515, 0.000000000000000000 ) ) ;
#78337=LINE ( 'NONE', #76938, #85836 ) ;
#78339=ORIENTED_EDGE ( 'NONE', *, *, #25702, .F. ) ;
#78341=ORIENTED_EDGE ( 'NONE', *, *, #140656, .F. ) ;
#78342=DIRECTION ( 'NONE',  ( -0.3543493200069162685, -0.000000000000000000, -0.9351131265310288487 ) ) ;
#78343=VECTOR ( 'NONE', #106415, 1000.000000000000227 ) ;
#78344=CARTESIAN_POINT ( 'NONE',  ( 24.48921356237309510, -27.52281430457072631, 5.000000000000000000 ) ) ;
#78345=AXIS2_PLACEMENT_3D ( 'NONE', #138725, #126394, #18316 ) ;
#78346=AXIS2_PLACEMENT_3D ( 'NONE', #50058, #137056, #16694 ) ;
#78347=EDGE_LOOP ( 'NONE', ( #11284, #129281, #66286, #112340 ) ) ;
#78348=ORIENTED_EDGE ( 'NONE', *, *, #24448, .F. ) ;
#78351=DIRECTION ( 'NONE',  ( -0.6830127018922180770, -0.6830127018922204085, -0.2588190451025213501 ) ) ;
#78352=ADVANCED_FACE ( 'NONE', ( #109513 ), #78325, .F. ) ;
#78353=FACE_OUTER_BOUND ( 'NONE', #24439, .T. ) ;
#78354=EDGE_CURVE ( 'NONE', #118868, #72669, #120345, .T. ) ;
#78356=EDGE_CURVE ( 'NONE', #58219, #15180, #21063, .T. ) ;
#78357=ORIENTED_EDGE ( 'NONE', *, *, #26972, .T. ) ;
#78359=EDGE_CURVE ( 'NONE', #136020, #137944, #44285, .T. ) ;
#78360=ORIENTED_EDGE ( 'NONE', *, *, #33814, .F. ) ;
#78361=ORIENTED_EDGE ( 'NONE', *, *, #125439, .T. ) ;
#78362=VECTOR ( 'NONE', #22373, 1000.000000000000227 ) ;
#78363=EDGE_LOOP ( 'NONE', ( #43289, #108413, #13558, #13660 ) ) ;
#78364=ADVANCED_FACE ( 'NONE', ( #108759 ), #97166, .F. ) ;
#78365=( BOUNDED_CURVE ( )  B_SPLINE_CURVE ( 3, ( #30394, #50722, #128983, #126831 ),
 .UNSPECIFIED., .F., .F. ) 
 B_SPLINE_CURVE_WITH_KNOTS ( ( 4, 4 ),
 ( 4.130769849943813909, 4.183600770845220751 ),
 .UNSPECIFIED. ) 
 CURVE ( )  GEOMETRIC_REPRESENTATION_ITEM ( )  RATIONAL_B_SPLINE_CURVE ( ( 1.000000000000000000, 0.9997674213408587196, 0.9997674213408587196, 1.000000000000000000 ) ) 
 REPRESENTATION_ITEM ( '' )  );
#78366=VECTOR ( 'NONE', #64914, 1000.000000000000000 ) ;
#78368=CARTESIAN_POINT ( 'NONE',  ( 24.18398860626899705, 28.73617430169804265, 5.000000000000000000 ) ) ;
#78369=VERTEX_POINT ( 'NONE', #67473 ) ;
#78370=DIRECTION ( 'NONE',  ( 0.3543493200069163240, -0.000000000000000000, 0.9351131265310288487 ) ) ;
#78373=LINE ( 'NONE', #66781, #99170 ) ;
#78374=CARTESIAN_POINT ( 'NONE',  ( -34.49999999999975131, 13.08746187583910547, 4.000000000000000000 ) ) ;
#78376=FACE_BOUND ( 'NONE', #29803, .T. ) ;
#78377=ORIENTED_EDGE ( 'NONE', *, *, #122164, .F. ) ;
#78378=ADVANCED_FACE ( 'NONE', ( #76920 ), #111664, .T. ) ;
#78379=LINE ( 'NONE', #56669, #36380 ) ;
#78380=LINE ( 'NONE', #135615, #92440 ) ;
#78381=PLANE ( 'NONE',  #76867 ) ;
#78382=LINE ( 'NONE', #132788, #106416 ) ;
#78383=ORIENTED_EDGE ( 'NONE', *, *, #100434, .F. ) ;
#78384=LINE ( 'NONE', #76983, #1787 ) ;
#78386=ORIENTED_EDGE ( 'NONE', *, *, #33113, .T. ) ;
#78387=ADVANCED_FACE ( 'NONE', ( #21792 ), #66040, .F. ) ;
#78388=ORIENTED_EDGE ( 'NONE', *, *, #222, .T. ) ;
#78390=VERTEX_POINT ( 'NONE', #33425 ) ;
#78391=CARTESIAN_POINT ( 'NONE',  ( 22.49999999999986144, 19.08746187583905041, 4.000000000000000000 ) ) ;
#78394=DIRECTION ( 'NONE',  ( 0.000000000000000000, -0.3543493200069152138, 0.9351131265310292928 ) ) ;
#78395=DIRECTION ( 'NONE',  ( -0.7071067811865486830, -0.7071067811865464625, 0.000000000000000000 ) ) ;
#78397=VECTOR ( 'NONE', #83439, 1000.000000000000000 ) ;
#78398=LINE ( 'NONE', #33491, #120304 ) ;
#78401=EDGE_LOOP ( 'NONE', ( #62553, #134736, #62661, #130822 ) ) ;
#78402=EDGE_CURVE ( 'NONE', #58607, #142587, #110205, .T. ) ;
#78403=ORIENTED_EDGE ( 'NONE', *, *, #91613, .T. ) ;
#78404=ORIENTED_EDGE ( 'NONE', *, *, #100655, .F. ) ;
#78405=EDGE_LOOP ( 'NONE', ( #74347, #6285, #20867, #59838, #132108 ) ) ;
#78407=VECTOR ( 'NONE', #67959, 999.9999999999998863 ) ;
#78408=CARTESIAN_POINT ( 'NONE',  ( 0.7071067811865432429, -0.7407075233842822515, 5.000000000000000000 ) ) ;
#78409=ORIENTED_EDGE ( 'NONE', *, *, #134903, .F. ) ;
#78410=VECTOR ( 'NONE', #78370, 1000.000000000000227 ) ;
#78411=ORIENTED_EDGE ( 'NONE', *, *, #60587, .T. ) ;
#78413=VECTOR ( 'NONE', #78808, 1000.000000000000000 ) ;
#78414=CARTESIAN_POINT ( 'NONE',  ( -4.828169399223491531, 0.7592924766157138627, 4.000000000000000000 ) ) ;
#78415=ORIENTED_EDGE ( 'NONE', *, *, #84100, .F. ) ;
#78416=CARTESIAN_POINT ( 'NONE',  ( 7.190181675744438117, -18.74070752338408852, 7.910009926591490270 ) ) ;
#78417=VECTOR ( 'NONE', #40152, 1000.000000000000227 ) ;
#78418=EDGE_CURVE ( 'NONE', #42016, #71242, #55147, .T. ) ;
#78419=PLANE ( 'NONE',  #118515 ) ;
#78421=DIRECTION ( 'NONE',  ( -0.7071067811865486830, -0.7071067811865464625, -0.000000000000000000 ) ) ;
#78422=VERTEX_POINT ( 'NONE', #121794 ) ;
#78424=CARTESIAN_POINT ( 'NONE',  ( 14.99999999999989697, 16.55218569542899587, 5.000000000000000000 ) ) ;
#78425=DIRECTION ( 'NONE',  ( -0.7071067811865486830, -0.7071067811865464625, 0.000000000000000000 ) ) ;
#78426=ADVANCED_FACE ( 'NONE', ( #22473 ), #100077, .T. ) ;
#78427=CARTESIAN_POINT ( 'NONE',  ( 0.7928932188134519832, 15.75929247661555976, 5.000000000000000000 ) ) ;
#78428=DIRECTION ( 'NONE',  ( 0.3543493200069162685, -0.000000000000000000, -0.9351131265310288487 ) ) ;
#78429=CARTESIAN_POINT ( 'NONE',  ( 1.358242975411386055, 15.75929247661555799, 19.34181609438699212 ) ) ;
#78430=VERTEX_POINT ( 'NONE', #92739 ) ;
#78431=AXIS2_PLACEMENT_3D ( 'NONE', #120477, #9590, #29926 ) ;
#78432=CARTESIAN_POINT ( 'NONE',  ( 0.000000000000000000, 0.000000000000000000, 5.000000000000000000 ) ) ;
#78434=ORIENTED_EDGE ( 'NONE', *, *, #86084, .T. ) ;
#78436=FACE_OUTER_BOUND ( 'NONE', #42256, .T. ) ;
#78437=FACE_OUTER_BOUND ( 'NONE', #75156, .T. ) ;
#78438=ORIENTED_EDGE ( 'NONE', *, *, #90649, .F. ) ;
#78439=LINE ( 'NONE', #101597, #85303 ) ;
#78440=VECTOR ( 'NONE', #64945, 1000.000000000000000 ) ;
#78441=EDGE_CURVE ( 'NONE', #44113, #24156, #106300, .T. ) ;
#78442=DIRECTION ( 'NONE',  ( -0.3543493200069162685, -0.000000000000000000, -0.9351131265310288487 ) ) ;
#78443=DIRECTION ( 'NONE',  ( -0.7071067811865487940, 0.7071067811865463515, -0.000000000000000000 ) ) ;
#78444=ORIENTED_EDGE ( 'NONE', *, *, #69469, .F. ) ;
#78445=AXIS2_PLACEMENT_3D ( 'NONE', #117479, #5139, #61727 ) ;
#78446=AXIS2_PLACEMENT_3D ( 'NONE', #61081, #94357, #8046 ) ;
#78447=DIRECTION ( 'NONE',  ( 0.6830127018922180770, -0.6830127018922204085, -0.2588190451025213501 ) ) ;
#78448=VECTOR ( 'NONE', #73125, 1000.000000000000227 ) ;
#78450=AXIS2_PLACEMENT_3D ( 'NONE', #141944, #74539, #118723 ) ;
#78451=DIRECTION ( 'NONE',  ( -0.000000000000000000, 0.3543493200069153248, 0.9351131265310292928 ) ) ;
#78452=CARTESIAN_POINT ( 'NONE',  ( -33.70710678118631165, 8.259292476615643253, 5.000000000000000000 ) ) ;
#78453=ORIENTED_EDGE ( 'NONE', *, *, #88420, .F. ) ;
#78454=EDGE_CURVE ( 'NONE', #11112, #123460, #36250, .T. ) ;
#78455=ORIENTED_EDGE ( 'NONE', *, *, #53280, .T. ) ;
#78457=CARTESIAN_POINT ( 'NONE',  ( 33.18398860626899705, 28.73617430169810305, 5.000000000000000000 ) ) ;
#78458=ORIENTED_EDGE ( 'NONE', *, *, #64998, .F. ) ;
#78459=VECTOR ( 'NONE', #46915, 1000.000000000000000 ) ;
#78460=CARTESIAN_POINT ( 'NONE',  ( -39.48921356237310221, -27.52281430457082934, 5.000000000000000000 ) ) ;
#78461=CARTESIAN_POINT ( 'NONE',  ( -26.72174548431410912, 8.259292476615641476, 11.78515199841144145 ) ) ;
#78462=DIRECTION ( 'NONE',  ( -1.000000000000000000, 4.620891819070403647E-14, 0.000000000000000000 ) ) ;
#78463=ORIENTED_EDGE ( 'NONE', *, *, #34768, .T. ) ;
#78464=CARTESIAN_POINT ( 'NONE',  ( 16.99806943317890529, -22.22500000000000142, 4.500000000000000888 ) ) ;
#78465=LINE ( 'NONE', #124811, #97583 ) ;
#78466=DIRECTION ( 'NONE',  ( -0.7071067811865486830, -0.7071067811865464625, 0.000000000000000000 ) ) ;
#78467=VECTOR ( 'NONE', #123582, 1000.000000000000000 ) ;
#78468=CARTESIAN_POINT ( 'NONE',  ( -2.510786437626908008, -27.52281430457053446, 5.000000000000000000 ) ) ;
#78470=PLANE ( 'NONE',  #9475 ) ;
#78471=ORIENTED_EDGE ( 'NONE', *, *, #53910, .F. ) ;
#78473=EDGE_CURVE ( 'NONE', #41252, #64397, #70345, .T. ) ;
#78474=VERTEX_POINT ( 'NONE', #71031 ) ;
#78475=ORIENTED_EDGE ( 'NONE', *, *, #118944, .F. ) ;
#78477=CARTESIAN_POINT ( 'NONE',  ( -25.49999999999981526, -17.94781430457063820, 5.000000000000000000 ) ) ;
#78478=CARTESIAN_POINT ( 'NONE',  ( -20.99999999999984368, 14.58746187583908771, 4.000000000000000000 ) ) ;
#78479=VERTEX_POINT ( 'NONE', #15171 ) ;
#78480=FACE_OUTER_BOUND ( 'NONE', #25460, .T. ) ;
#78481=DIRECTION ( 'NONE',  ( -0.000000000000000000, 0.000000000000000000, 1.000000000000000000 ) ) ;
#78482=CARTESIAN_POINT ( 'NONE',  ( 0.000000000000000000, 0.000000000000000000, 5.000000000000000000 ) ) ;
#78483=LINE ( 'NONE', #46619, #23286 ) ;
#78485=VERTEX_POINT ( 'NONE', #80479 ) ;
#78486=EDGE_CURVE ( 'NONE', #132165, #27437, #79073, .T. ) ;
#78487=CARTESIAN_POINT ( 'NONE',  ( 7.499999999999951150, -14.94781430457067906, 5.000000000000000000 ) ) ;
#78488=PLANE ( 'NONE',  #24073 ) ;
#78489=DIRECTION ( 'NONE',  ( 0.7071067811865487940, 0.7071067811865463515, 0.000000000000000000 ) ) ;
#78490=FACE_OUTER_BOUND ( 'NONE', #62483, .T. ) ;
#78491=PLANE ( 'NONE',  #118610 ) ;
#78492=CARTESIAN_POINT ( 'NONE',  ( 25.36246187583883582, 22.22500000000000853, 4.000000000000000000 ) ) ;
#78494=LINE ( 'NONE', #143029, #44525 ) ;
#78495=DIRECTION ( 'NONE',  ( 0.6830127018922181881, 0.6830127018922202975, -0.2588190451025214056 ) ) ;
#78496=ORIENTED_EDGE ( 'NONE', *, *, #88142, .F. ) ;
#78497=ORIENTED_EDGE ( 'NONE', *, *, #85028, .T. ) ;
#78499=CARTESIAN_POINT ( 'NONE',  ( -30.32816939922331656, -0.7407075233842770334, 4.000000000000000000 ) ) ;
#78500=CARTESIAN_POINT ( 'NONE',  ( -6.183988606268994381, 28.73617430169791476, 5.000000000000000000 ) ) ;
#78501=ORIENTED_EDGE ( 'NONE', *, *, #101835, .F. ) ;
#78502=DIRECTION ( 'NONE',  ( 0.6830127018922180770, -0.6830127018922204085, -0.2588190451025213501 ) ) ;
#78503=EDGE_CURVE ( 'NONE', #39995, #15337, #45720, .T. ) ;
#78504=CARTESIAN_POINT ( 'NONE',  ( 45.48921356237309510, -27.52281430457087197, 5.000000000000000000 ) ) ;
#78506=VERTEX_POINT ( 'NONE', #2137 ) ;
#78507=CARTESIAN_POINT ( 'NONE',  ( -34.45011844616454511, -4.483719188362475627, 5.000000000000000888 ) ) ;
#78508=VERTEX_POINT ( 'NONE', #56618 ) ;
#78509=ORIENTED_EDGE ( 'NONE', *, *, #26545, .T. ) ;
#78510=LINE ( 'NONE', #3755, #12480 ) ;
#78511=VECTOR ( 'NONE', #51114, 1000.000000000000000 ) ;
#78514=FACE_OUTER_BOUND ( 'NONE', #86847, .T. ) ;
#78516=AXIS2_PLACEMENT_3D ( 'NONE', #83366, #72536, #17380 ) ;
#78518=ORIENTED_EDGE ( 'NONE', *, *, #135014, .T. ) ;
#78519=LINE ( 'NONE', #15878, #16403 ) ;
#78520=ORIENTED_EDGE ( 'NONE', *, *, #120226, .T. ) ;
#78521=DIRECTION ( 'NONE',  ( 0.7071067811865486830, -0.7071067811865464625, -0.000000000000000000 ) ) ;
#78525=DIRECTION ( 'NONE',  ( -0.000000000000000000, 0.3543493200069153248, 0.9351131265310292928 ) ) ;
#78526=LINE ( 'NONE', #36448, #85510 ) ;
#78527=VECTOR ( 'NONE', #143531, 1000.000000000000227 ) ;
#78528=EDGE_CURVE ( 'NONE', #80339, #28555, #14485, .T. ) ;
#78529=EDGE_LOOP ( 'NONE', ( #33009, #109224, #80756, #81584, #121400, #93855 ) ) ;
#78531=CARTESIAN_POINT ( 'NONE',  ( 0.000000000000000000, 0.000000000000000000, 5.000000000000000000 ) ) ;
#78533=EDGE_CURVE ( 'NONE', #141976, #66880, #22065, .T. ) ;
#78534=FACE_OUTER_BOUND ( 'NONE', #71148, .T. ) ;
#78535=EDGE_CURVE ( 'NONE', #113749, #114341, #136980, .T. ) ;
#78536=CARTESIAN_POINT ( 'NONE',  ( 6.183988606268994381, 28.73617430169791476, 5.000000000000000000 ) ) ;
#78537=ORIENTED_EDGE ( 'NONE', *, *, #34550, .T. ) ;
#78539=CARTESIAN_POINT ( 'NONE',  ( 18.18398860626898994, 28.73617430169800002, 5.000000000000000000 ) ) ;
#78540=ORIENTED_EDGE ( 'NONE', *, *, #42409, .F. ) ;
#78541=EDGE_CURVE ( 'NONE', #40388, #57093, #37686, .T. ) ;
#78542=VECTOR ( 'NONE', #70672, 1000.000000000000000 ) ;
#78543=DIRECTION ( 'NONE',  ( -0.000000000000000000, 0.3543493200069153248, 0.9351131265310292928 ) ) ;
#78544=ORIENTED_EDGE ( 'NONE', *, *, #121412, .T. ) ;
#78545=DIRECTION ( 'NONE',  ( 0.7071067811865487940, 0.7071067811865463515, -0.000000000000000000 ) ) ;
#78546=LINE ( 'NONE', #952, #64146 ) ;
#78547=DIRECTION ( 'NONE',  ( 0.6830127018922181881, 0.6830127018922202975, -0.2588190451025214056 ) ) ;
#78549=VECTOR ( 'NONE', #82238, 1000.000000000000000 ) ;
#78550=CARTESIAN_POINT ( 'NONE',  ( -22.49999999999984013, -2.568876922607784774, 4.000000000000000000 ) ) ;
#78551=VECTOR ( 'NONE', #22775, 1000.000000000000227 ) ;
#78552=EDGE_CURVE ( 'NONE', #61902, #103852, #34826, .T. ) ;
#78553=FACE_BOUND ( 'NONE', #55546, .T. ) ;
#78555=CARTESIAN_POINT ( 'NONE',  ( 34.92499999999998295, -16.48753812416035203, 4.000000000000000000 ) ) ;
#78556=CARTESIAN_POINT ( 'NONE',  ( -24.18398860626899705, 28.73617430169804265, 5.000000000000000000 ) ) ;
#78557=CARTESIAN_POINT ( 'NONE',  ( 27.48921356237309155, -27.52281430457074762, 5.000000000000000000 ) ) ;
#78558=CARTESIAN_POINT ( 'NONE',  ( -24.48921356237309510, -27.52281430457072631, 5.000000000000000000 ) ) ;
#78559=ORIENTED_EDGE ( 'NONE', *, *, #87304, .F. ) ;
#78561=VECTOR ( 'NONE', #87150, 1000.000000000000000 ) ;
#78562=LINE ( 'NONE', #32938, #16214 ) ;
#78564=ORIENTED_EDGE ( 'NONE', *, *, #125500, .T. ) ;
#78565=ORIENTED_EDGE ( 'NONE', *, *, #32180, .F. ) ;
#78567=ORIENTED_EDGE ( 'NONE', *, *, #101761, .T. ) ;
#78568=FACE_OUTER_BOUND ( 'NONE', #91378, .T. ) ;
#78569=CARTESIAN_POINT ( 'NONE',  ( 34.42499999999998295, 0.000000000000000000, 4.500000000000000888 ) ) ;
#78571=DIRECTION ( 'NONE',  ( -1.000000000000000000, 0.000000000000000000, -0.000000000000000000 ) ) ;
#78572=EDGE_CURVE ( 'NONE', #82088, #5782, #79797, .T. ) ;
#78574=DIRECTION ( 'NONE',  ( -0.7071067811865487940, 0.7071067811865463515, -0.000000000000000000 ) ) ;
#78575=CARTESIAN_POINT ( 'NONE',  ( 2.700255128608413990, -27.71228299555204089, 4.000000000000000000 ) ) ;
#78576=FACE_OUTER_BOUND ( 'NONE', #68951, .T. ) ;
#78577=ORIENTED_EDGE ( 'NONE', *, *, #54485, .T. ) ;
#78578=EDGE_CURVE ( 'NONE', #92260, #96833, #113069, .T. ) ;
#78579=ORIENTED_EDGE ( 'NONE', *, *, #126146, .T. ) ;
#78580=CYLINDRICAL_SURFACE ( 'NONE', #65907, 0.5000000000000004441 ) ;
#78582=VERTEX_POINT ( 'NONE', #102931 ) ;
#78583=VERTEX_POINT ( 'NONE', #3572 ) ;
#78584=ORIENTED_EDGE ( 'NONE', *, *, #77263, .F. ) ;
#78585=DIRECTION ( 'NONE',  ( 0.7071067811865486830, -0.7071067811865464625, -0.000000000000000000 ) ) ;
#78587=ORIENTED_EDGE ( 'NONE', *, *, #48362, .F. ) ;
#78588=CARTESIAN_POINT ( 'NONE',  ( 12.09667064187398111, -2.240707523384257716, 15.26439735382755281 ) ) ;
#78589=EDGE_CURVE ( 'NONE', #77094, #128364, #92031, .T. ) ;
#78593=ORIENTED_EDGE ( 'NONE', *, *, #109642, .F. ) ;
#78594=DIRECTION ( 'NONE',  ( -0.7071067811865487940, 0.7071067811865463515, -0.000000000000000000 ) ) ;
#78595=CARTESIAN_POINT ( 'NONE',  ( -36.48921356237310221, -27.52281430457080802, 5.000000000000000000 ) ) ;
#78596=DIRECTION ( 'NONE',  ( 0.6830127018922181881, 0.6830127018922202975, -0.2588190451025214056 ) ) ;
#78597=DIRECTION ( 'NONE',  ( -0.3543493200069162685, -0.000000000000000000, -0.9351131265310288487 ) ) ;
#78598=ORIENTED_EDGE ( 'NONE', *, *, #29135, .T. ) ;
#78599=ORIENTED_EDGE ( 'NONE', *, *, #114218, .F. ) ;
#78601=CARTESIAN_POINT ( 'NONE',  ( 27.32816939922334143, 20.25929247661551003, 4.000000000000000000 ) ) ;
#78602=EDGE_LOOP ( 'NONE', ( #47883, #113942, #133268, #34876 ) ) ;
#78603=CARTESIAN_POINT ( 'NONE',  ( -26.99999999999980815, -22.22500000000000142, 4.412002311790036657 ) ) ;
#78604=CARTESIAN_POINT ( 'NONE',  ( -8.207106781186482181, -5.240707523384228850, 5.000000000000000000 ) ) ;
#78605=ORIENTED_EDGE ( 'NONE', *, *, #98197, .T. ) ;
#78606=EDGE_CURVE ( 'NONE', #136324, #133168, #89892, .T. ) ;
#78607=DIRECTION ( 'NONE',  ( 0.7071067811865486830, -0.7071067811865464625, -0.000000000000000000 ) ) ;
#78609=CARTESIAN_POINT ( 'NONE',  ( 12.29974487139158512, -27.71228299555214747, 4.000000000000000000 ) ) ;
#78610=AXIS2_PLACEMENT_3D ( 'NONE', #37948, #115442, #16135 ) ;
#78615=DIRECTION ( 'NONE',  ( -0.000000000000000000, 0.000000000000000000, 1.000000000000000000 ) ) ;
#78616=VECTOR ( 'NONE', #24354, 1000.000000000000227 ) ;
#78617=CARTESIAN_POINT ( 'NONE',  ( -0.005480084712502889671, 28.92564299267938210, 4.000000000000000000 ) ) ;
#78618=CARTESIAN_POINT ( 'NONE',  ( -27.83829387547363510, -6.740707523384205757, 16.75550250614860914 ) ) ;
#78619=ORIENTED_EDGE ( 'NONE', *, *, #110021, .F. ) ;
#78620=EDGE_CURVE ( 'NONE', #139077, #5268, #134138, .T. ) ;
#78621=ORIENTED_EDGE ( 'NONE', *, *, #105560, .F. ) ;
#78622=CARTESIAN_POINT ( 'NONE',  ( 3.489213562373097322, -27.52281430457057709, 5.000000000000000000 ) ) ;
#78624=LINE ( 'NONE', #122837, #138555 ) ;
#78625=PLANE ( 'NONE',  #45147 ) ;
#78626=CARTESIAN_POINT ( 'NONE',  ( -34.92500000000001137, -3.281509562795737800, 4.759050581649335143 ) ) ;
#78628=VECTOR ( 'NONE', #37622, 1000.000000000000227 ) ;
#78629=DIRECTION ( 'NONE',  ( -0.7071067811865486830, 0.7071067811865464625, 0.000000000000000000 ) ) ;
#78630=CARTESIAN_POINT ( 'NONE',  ( -34.92500000000001137, -22.22500000000000142, 4.000000000000000000 ) ) ;
#78631=ORIENTED_EDGE ( 'NONE', *, *, #77217, .T. ) ;
#78632=LINE ( 'NONE', #2460, #125214 ) ;
#78633=CARTESIAN_POINT ( 'NONE',  ( -34.92500000000001137, 21.72500000000000142, 5.000000000000000000 ) ) ;
#78634=DIRECTION ( 'NONE',  ( -0.000000000000000000, 0.3543493200069153248, 0.9351131265310292928 ) ) ;
#78635=VECTOR ( 'NONE', #99853, 999.9999999999998863 ) ;
#78636=VECTOR ( 'NONE', #99132, 1000.000000000000000 ) ;
#78637=PLANE ( 'NONE',  #89833 ) ;
#78641=LINE ( 'NONE', #21407, #27986 ) ;
#78642=EDGE_CURVE ( 'NONE', #133340, #13138, #28222, .T. ) ;
#78643=ORIENTED_EDGE ( 'NONE', *, *, #29604, .F. ) ;
#78645=ORIENTED_EDGE ( 'NONE', *, *, #112266, .T. ) ;
#78646=CARTESIAN_POINT ( 'NONE',  ( 8.292893218813404133, -12.74070752338415247, 5.000000000000000000 ) ) ;
#78647=VECTOR ( 'NONE', #122727, 999.9999999999998863 ) ;
#78648=VECTOR ( 'NONE', #137678, 999.9999999999998863 ) ;
#78649=PLANE ( 'NONE',  #103963 ) ;
#78650=DIRECTION ( 'NONE',  ( -0.000000000000000000, -0.3543493200069152693, 0.9351131265310292928 ) ) ;
#78651=LINE ( 'NONE', #33041, #87868 ) ;
#78652=ADVANCED_FACE ( 'NONE', ( #126792 ), #105739, .F. ) ;
#78653=CARTESIAN_POINT ( 'NONE',  ( -34.49999999999976552, 13.46425560840034841, 4.994342998332165884 ) ) ;
#78654=DIRECTION ( 'NONE',  ( -0.7071067811865487940, 0.7071067811865463515, -0.000000000000000000 ) ) ;
#78655=ORIENTED_EDGE ( 'NONE', *, *, #111043, .T. ) ;
#78656=VECTOR ( 'NONE', #129863, 1000.000000000000000 ) ;
#78657=ADVANCED_FACE ( 'NONE', ( #116643 ), #27478, .F. ) ;
#78658=ORIENTED_EDGE ( 'NONE', *, *, #38670, .F. ) ;
#78659=CARTESIAN_POINT ( 'NONE',  ( -33.18398860626899705, 28.73617430169810305, 5.000000000000000000 ) ) ;
#78660=VECTOR ( 'NONE', #116283, 1000.000000000000000 ) ;
#78661=CARTESIAN_POINT ( 'NONE',  ( -13.77797537283184326, 22.22500000000000142, 13.01339814852647869 ) ) ;
#78662=PLANE ( 'NONE',  #126950 ) ;
#78664=DIRECTION ( 'NONE',  ( 0.6830127018922181881, 0.6830127018922202975, -0.2588190451025214056 ) ) ;
#78665=PLANE ( 'NONE',  #131729 ) ;
#78666=EDGE_LOOP ( 'NONE', ( #80858, #123415, #96506, #111322 ) ) ;
#78668=ADVANCED_FACE ( 'NONE', ( #84733 ), #18005, .F. ) ;
#78670=LINE ( 'NONE', #122146, #69465 ) ;
#78671=FACE_OUTER_BOUND ( 'NONE', #7234, .T. ) ;
#78673=VERTEX_POINT ( 'NONE', #60153 ) ;
#78674=ADVANCED_FACE ( 'NONE', ( #73170 ), #40533, .F. ) ;
#78675=LINE ( 'NONE', #125760, #120802 ) ;
#78676=DIRECTION ( 'NONE',  ( 1.000000000000000000, 0.000000000000000000, 0.000000000000000000 ) ) ;
#78678=ORIENTED_EDGE ( 'NONE', *, *, #80232, .F. ) ;
#78679=ORIENTED_EDGE ( 'NONE', *, *, #5178, .F. ) ;
#78680=LINE ( 'NONE', #104528, #132406 ) ;
#78681=CARTESIAN_POINT ( 'NONE',  ( 27.15612307739222331, -22.22500000000000142, 4.000000000000000000 ) ) ;
#78682=LINE ( 'NONE', #124320, #27816 ) ;
#78683=CARTESIAN_POINT ( 'NONE',  ( 14.51078643762690490, -27.52281430457045275, 5.000000000000000000 ) ) ;
#78684=FACE_OUTER_BOUND ( 'NONE', #142005, .T. ) ;
#78685=EDGE_LOOP ( 'NONE', ( #72488, #82675, #93616, #49416 ) ) ;
#78687=CARTESIAN_POINT ( 'NONE',  ( -31.80981832425532829, -18.74070752338408852, 7.910009926591581753 ) ) ;
#78688=CARTESIAN_POINT ( 'NONE',  ( -18.29974487139159223, -27.71228299555219010, 4.000000000000000000 ) ) ;
#78689=EDGE_CURVE ( 'NONE', #54392, #22559, #94166, .T. ) ;
#78690=CARTESIAN_POINT ( 'NONE',  ( 32.29289321881323360, -0.7407075233842770334, 5.000000000000000000 ) ) ;
#78692=VERTEX_POINT ( 'NONE', #17329 ) ;
#78693=EDGE_CURVE ( 'NONE', #99319, #29884, #84057, .T. ) ;
#78696=ORIENTED_EDGE ( 'NONE', *, *, #7414, .T. ) ;
#78698=EDGE_CURVE ( 'NONE', #17086, #33380, #63015, .T. ) ;
#78699=CARTESIAN_POINT ( 'NONE',  ( 18.48921356237309510, -27.52281430457068367, 5.000000000000000000 ) ) ;
#78700=DIRECTION ( 'NONE',  ( 1.000000000000000000, 0.000000000000000000, 0.000000000000000000 ) ) ;
#78701=LINE ( 'NONE', #47551, #124254 ) ;
#78703=VERTEX_POINT ( 'NONE', #85424 ) ;
#78704=DIRECTION ( 'NONE',  ( 0.3543493200069162685, -0.000000000000000000, -0.9351131265310288487 ) ) ;
#78706=ADVANCED_FACE ( 'NONE', ( #74593 ), #39837, .T. ) ;
#78707=EDGE_CURVE ( 'NONE', #15358, #44633, #117333, .T. ) ;
#78708=VECTOR ( 'NONE', #112825, 999.9999999999998863 ) ;
#78709=ORIENTED_EDGE ( 'NONE', *, *, #137011, .T. ) ;
#78710=LINE ( 'NONE', #1804, #65311 ) ;
#78711=PLANE ( 'NONE',  #138237 ) ;
#78712=DIRECTION ( 'NONE',  ( 1.000000000000000000, -0.000000000000000000, -0.000000000000000000 ) ) ;
#78713=VECTOR ( 'NONE', #104421, 1000.000000000000000 ) ;
#78715=AXIS2_PLACEMENT_3D ( 'NONE', #107302, #65263, #29728 ) ;
#78716=ORIENTED_EDGE ( 'NONE', *, *, #16416, .T. ) ;
#78717=AXIS2_PLACEMENT_3D ( 'NONE', #105994, #116192, #50235 ) ;
#78718=EDGE_CURVE ( 'NONE', #88501, #24531, #83319, .T. ) ;
#78719=FACE_BOUND ( 'NONE', #20822, .T. ) ;
#78720=ADVANCED_FACE ( 'NONE', ( #129653 ), #106444, .F. ) ;
#78721=FACE_OUTER_BOUND ( 'NONE', #9078, .T. ) ;
#78722=DIRECTION ( 'NONE',  ( 1.000000000000000000, 0.000000000000000000, 0.000000000000000000 ) ) ;
#78723=CARTESIAN_POINT ( 'NONE',  ( -60.48921356237309510, -27.52281430457097500, 5.000000000000000000 ) ) ;
#78724=AXIS2_PLACEMENT_3D ( 'NONE', #140016, #63187, #82769 ) ;
#78726=CARTESIAN_POINT ( 'NONE',  ( 23.81601139373100295, 28.73617430169770870, 5.000000000000000000 ) ) ;
#78728=ORIENTED_EDGE ( 'NONE', *, *, #1078, .F. ) ;
#78729=ORIENTED_EDGE ( 'NONE', *, *, #126938, .T. ) ;
#78731=ORIENTED_EDGE ( 'NONE', *, *, #50244, .T. ) ;
#78732=ADVANCED_FACE ( 'NONE', ( #61586 ), #139133, .T. ) ;
#78735=VECTOR ( 'NONE', #123438, 1000.000000000000114 ) ;
#78736=VECTOR ( 'NONE', #132551, 1000.000000000000227 ) ;
#78737=PLANE ( 'NONE',  #111768 ) ;
#78738=ADVANCED_FACE ( 'NONE', ( #49287 ), #137708, .F. ) ;
#78740=VECTOR ( 'NONE', #41586, 1000.000000000000000 ) ;
#78741=PLANE ( 'NONE',  #98102 ) ;
#78743=CARTESIAN_POINT ( 'NONE',  ( 34.49999999999975842, -17.94567065516886117, 4.994342998332151673 ) ) ;
#78744=DIRECTION ( 'NONE',  ( 0.7071067811865487940, 0.7071067811865463515, 0.000000000000000000 ) ) ;
#78745=CARTESIAN_POINT ( 'NONE',  ( 19.49999999999985789, -1.592773361805355226, -6.492772025301275285 ) ) ;
#78746=CARTESIAN_POINT ( 'NONE',  ( -14.81601139373099585, 28.73617430169776910, 5.000000000000000000 ) ) ;
#78747=DIRECTION ( 'NONE',  ( -0.6830127018922180770, -0.6830127018922204085, -0.2588190451025213501 ) ) ;
#78748=VECTOR ( 'NONE', #108377, 1000.000000000000000 ) ;
#78750=EDGE_CURVE ( 'NONE', #94433, #135400, #11415, .T. ) ;
#78751=CARTESIAN_POINT ( 'NONE',  ( -20.51078643762690490, -27.52281430457041012, 5.000000000000000000 ) ) ;
#78752=ORIENTED_EDGE ( 'NONE', *, *, #106659, .T. ) ;
#78753=VECTOR ( 'NONE', #59441, 1000.000000000000000 ) ;
#78754=PLANE ( 'NONE',  #100543 ) ;
#78756=ORIENTED_EDGE ( 'NONE', *, *, #6850, .F. ) ;
#78757=ORIENTED_EDGE ( 'NONE', *, *, #77906, .F. ) ;
#78758=VECTOR ( 'NONE', #69439, 1000.000000000000000 ) ;
#78759=ORIENTED_EDGE ( 'NONE', *, *, #25118, .F. ) ;
#78763=ORIENTED_EDGE ( 'NONE', *, *, #5505, .T. ) ;
#78764=CARTESIAN_POINT ( 'NONE',  ( 17.99999999999987921, 14.96639925780210412, 5.000000000000000000 ) ) ;
#78765=EDGE_CURVE ( 'NONE', #86499, #86210, #65152, .T. ) ;
#78766=VECTOR ( 'NONE', #51102, 999.9999999999998863 ) ;
#78769=CARTESIAN_POINT ( 'NONE',  ( -20.70025512860841133, -27.71228299555191654, 4.000000000000000000 ) ) ;
#78770=VERTEX_POINT ( 'NONE', #20164 ) ;
#78771=CARTESIAN_POINT ( 'NONE',  ( 30.48921356237309510, -27.52281430457076894, 5.000000000000000000 ) ) ;
#78773=CARTESIAN_POINT ( 'NONE',  ( 0.1839886062690032631, 28.73617430169787568, 5.000000000000000000 ) ) ;
#78774=VECTOR ( 'NONE', #41382, 1000.000000000000000 ) ;
#78775=EDGE_CURVE ( 'NONE', #88325, #72440, #87592, .T. ) ;
#78777=ORIENTED_EDGE ( 'NONE', *, *, #38259, .T. ) ;
#78780=CARTESIAN_POINT ( 'NONE',  ( 11.67183060077639212, -0.7407075233842701500, 4.000000000000000000 ) ) ;
#78781=EDGE_LOOP ( 'NONE', ( #139392, #9893, #60334, #71748 ) ) ;
#78782=PLANE ( 'NONE',  #105998 ) ;
#78785=ORIENTED_EDGE ( 'NONE', *, *, #43496, .F. ) ;
#78787=VECTOR ( 'NONE', #111185, 1000.000000000000227 ) ;
#78788=CARTESIAN_POINT ( 'NONE',  ( 0.000000000000000000, 0.000000000000000000, 5.000000000000000000 ) ) ;
#78789=CARTESIAN_POINT ( 'NONE',  ( -28.49999999999979750, 16.77039438581776665, 0.4657186855308382278 ) ) ;
#78790=LINE ( 'NONE', #34568, #48698 ) ;
#78793=AXIS2_PLACEMENT_3D ( 'NONE', #43180, #9050, #29418 ) ;
#78795=CARTESIAN_POINT ( 'NONE',  ( 0.000000000000000000, 0.000000000000000000, 5.000000000000000000 ) ) ;
#78797=PLANE ( 'NONE',  #9112 ) ;
#78798=LINE ( 'NONE', #136015, #87711 ) ;
#78799=FACE_OUTER_BOUND ( 'NONE', #4338, .T. ) ;
#78800=ORIENTED_EDGE ( 'NONE', *, *, #20444, .T. ) ;
#78801=ORIENTED_EDGE ( 'NONE', *, *, #99420, .F. ) ;
#78803=ORIENTED_EDGE ( 'NONE', *, *, #133303, .T. ) ;
#78805=PLANE ( 'NONE',  #53345 ) ;
#78807=VECTOR ( 'NONE', #93246, 1000.000000000000000 ) ;
#78808=DIRECTION ( 'NONE',  ( 0.7071067811865486830, -0.7071067811865464625, -0.000000000000000000 ) ) ;
#78811=VECTOR ( 'NONE', #134522, 1000.000000000000000 ) ;
#78812=CARTESIAN_POINT ( 'NONE',  ( 16.49999999999988276, -17.91344420646041158, 1.358650452708503709 ) ) ;
#78814=CARTESIAN_POINT ( 'NONE',  ( 33.18398860626899705, 28.73617430169810305, 5.000000000000000000 ) ) ;
#78815=DIRECTION ( 'NONE',  ( -0.6830127018922181881, 0.6830127018922202975, -0.2588190451025214056 ) ) ;
#78816=VERTEX_POINT ( 'NONE', #42686 ) ;
#78818=VECTOR ( 'NONE', #104546, 1000.000000000000000 ) ;
#78819=ORIENTED_EDGE ( 'NONE', *, *, #122834, .F. ) ;
#78820=VECTOR ( 'NONE', #106366, 1000.000000000000227 ) ;
#78825=ORIENTED_EDGE ( 'NONE', *, *, #108815, .T. ) ;
#78826=( BOUNDED_CURVE ( )  B_SPLINE_CURVE ( 3, ( #103847, #16880, #49539, #16120 ),
 .UNSPECIFIED., .F., .T. ) 
 B_SPLINE_CURVE_WITH_KNOTS ( ( 4, 4 ),
 ( 5.135034128376270601, 5.164990091338616196 ),
 .UNSPECIFIED. ) 
 CURVE ( )  GEOMETRIC_REPRESENTATION_ITEM ( )  RATIONAL_B_SPLINE_CURVE ( ( 1.000000000000000000, 0.9999252214215840207, 0.9999252214215840207, 1.000000000000000000 ) ) 
 REPRESENTATION_ITEM ( '' )  );
#78829=DIRECTION ( 'NONE',  ( -0.000000000000000000, 0.000000000000000000, 1.000000000000000000 ) ) ;
#78830=VERTEX_POINT ( 'NONE', #66563 ) ;
#78833=PLANE ( 'NONE',  #102776 ) ;
#78834=ORIENTED_EDGE ( 'NONE', *, *, #94110, .F. ) ;
#78837=ORIENTED_EDGE ( 'NONE', *, *, #88654, .F. ) ;
#78838=LINE ( 'NONE', #36052, #81428 ) ;
#78840=ORIENTED_EDGE ( 'NONE', *, *, #57302, .T. ) ;
#78841=EDGE_CURVE ( 'NONE', #121292, #6949, #44853, .T. ) ;
#78842=CARTESIAN_POINT ( 'NONE',  ( -26.99451991528749417, 28.92564299267956685, 4.000000000000000000 ) ) ;
#78845=CARTESIAN_POINT ( 'NONE',  ( -27.48921356237309155, -27.52281430457074762, 5.000000000000000000 ) ) ;
#78846=EDGE_LOOP ( 'NONE', ( #41046, #3708, #114702, #23443, #81323 ) ) ;
#78849=CARTESIAN_POINT ( 'NONE',  ( 28.82816939922332722, 6.759292476615644141, 4.000000000000000000 ) ) ;
#78850=PLANE ( 'NONE',  #115551 ) ;
#78853=VECTOR ( 'NONE', #68191, 999.9999999999998863 ) ;
#78854=DIRECTION ( 'NONE',  ( -0.7071067811865486830, -0.7071067811865464625, 0.000000000000000000 ) ) ;
#78855=CARTESIAN_POINT ( 'NONE',  ( 18.18398860626898994, 28.73617430169800002, 5.000000000000000000 ) ) ;
#78856=ORIENTED_EDGE ( 'NONE', *, *, #113959, .F. ) ;
#78857=ORIENTED_EDGE ( 'NONE', *, *, #74624, .F. ) ;
#78858=EDGE_CURVE ( 'NONE', #13678, #57193, #33257, .T. ) ;
#78859=AXIS2_PLACEMENT_3D ( 'NONE', #38578, #15357, #59642 ) ;
#78860=LINE ( 'NONE', #13549, #69842 ) ;
#78862=VECTOR ( 'NONE', #92815, 1000.000000000000000 ) ;
#78864=AXIS2_PLACEMENT_3D ( 'NONE', #111659, #123971, #122512 ) ;
#78865=FACE_OUTER_BOUND ( 'NONE', #73038, .T. ) ;
#78867=DIRECTION ( 'NONE',  ( 0.7071067811865487940, -0.7071067811865463515, 0.000000000000000000 ) ) ;
#78868=DIRECTION ( 'NONE',  ( 0.7071067811865487940, -0.7071067811865463515, 0.000000000000000000 ) ) ;
#78869=ORIENTED_EDGE ( 'NONE', *, *, #140665, .F. ) ;
#78870=EDGE_CURVE ( 'NONE', #78244, #125983, #118779, .T. ) ;
#78871=VECTOR ( 'NONE', #119789, 999.9999999999998863 ) ;
#78874=DIRECTION ( 'NONE',  ( 0.6830127018922180770, -0.6830127018922204085, -0.2588190451025213501 ) ) ;
#78875=FACE_OUTER_BOUND ( 'NONE', #138578, .T. ) ;
#78877=FACE_OUTER_BOUND ( 'NONE', #120501, .T. ) ;
#78878=ORIENTED_EDGE ( 'NONE', *, *, #102063, .F. ) ;
#78882=CARTESIAN_POINT ( 'NONE',  ( 24.48921356237309510, -27.52281430457072631, 5.000000000000000000 ) ) ;
#78883=ADVANCED_FACE ( 'NONE', ( #141996 ), #91192, .T. ) ;
#78884=CARTESIAN_POINT ( 'NONE',  ( 14.99451991528749595, 28.92564299267948513, 4.000000000000000000 ) ) ;
#78885=LINE ( 'NONE', #34649, #104702 ) ;
#78886=EDGE_LOOP ( 'NONE', ( #114000, #117369, #131465, #63940 ) ) ;
#78887=ORIENTED_EDGE ( 'NONE', *, *, #4358, .T. ) ;
#78888=ORIENTED_EDGE ( 'NONE', *, *, #63217, .T. ) ;
#78893=ADVANCED_FACE ( 'NONE', ( #48367 ), #47005, .F. ) ;
#78895=VECTOR ( 'NONE', #120165, 999.9999999999998863 ) ;
#78896=DIRECTION ( 'NONE',  ( -0.7071067811865487940, 0.7071067811865463515, -0.000000000000000000 ) ) ;
#78897=CARTESIAN_POINT ( 'NONE',  ( -20.99451991528748707, 28.92564299267952777, 4.000000000000000000 ) ) ;
#78899=DIRECTION ( 'NONE',  ( -0.6830127018922181881, 0.6830127018922202975, -0.2588190451025214056 ) ) ;
#78900=DIRECTION ( 'NONE',  ( 0.000000000000000000, 0.3543493200069153248, 0.9351131265310291818 ) ) ;
#78901=EDGE_CURVE ( 'NONE', #80773, #140269, #58593, .T. ) ;
#78902=EDGE_CURVE ( 'NONE', #80281, #45110, #57141, .T. ) ;
#78905=VERTEX_POINT ( 'NONE', #92560 ) ;
#78906=LINE ( 'NONE', #102787, #11851 ) ;
#78907=LINE ( 'NONE', #23792, #74761 ) ;
#78908=VECTOR ( 'NONE', #44204, 999.9999999999998863 ) ;
#78909=EDGE_CURVE ( 'NONE', #122922, #72201, #69429, .T. ) ;
#78910=ORIENTED_EDGE ( 'NONE', *, *, #71640, .F. ) ;
#78911=VERTEX_POINT ( 'NONE', #114334 ) ;
#78912=DIRECTION ( 'NONE',  ( 0.6830127018922181881, 0.6830127018922202975, -0.2588190451025214056 ) ) ;
#78913=EDGE_CURVE ( 'NONE', #40388, #122448, #136088, .T. ) ;
#78915=DIRECTION ( 'NONE',  ( -0.7071067811865487940, 0.7071067811865463515, -0.000000000000000000 ) ) ;
#78916=AXIS2_PLACEMENT_3D ( 'NONE', #126959, #16029, #58925 ) ;
#78919=DIRECTION ( 'NONE',  ( -0.3543493200069162685, -0.000000000000000000, -0.9351131265310288487 ) ) ;
#78920=ORIENTED_EDGE ( 'NONE', *, *, #50756, .F. ) ;
#78921=ORIENTED_EDGE ( 'NONE', *, *, #69245, .T. ) ;
#78922=EDGE_CURVE ( 'NONE', #84015, #5780, #122332, .T. ) ;
#78923=CARTESIAN_POINT ( 'NONE',  ( -34.82816939922328459, -2.240707523384260824, 4.000000000000000000 ) ) ;
#78924=ORIENTED_EDGE ( 'NONE', *, *, #114224, .F. ) ;
#78926=VECTOR ( 'NONE', #16760, 1000.000000000000227 ) ;
#78927=ADVANCED_FACE ( 'NONE', ( #123090 ), #45550, .F. ) ;
#78928=VECTOR ( 'NONE', #76804, 999.9999999999998863 ) ;
#78929=VECTOR ( 'NONE', #7726, 1000.000000000000000 ) ;
#78930=DIRECTION ( 'NONE',  ( -0.3543493200069162685, -0.000000000000000000, -0.9351131265310288487 ) ) ;
#78931=EDGE_LOOP ( 'NONE', ( #21256, #108746, #54719, #40350, #113971 ) ) ;
#78934=DIRECTION ( 'NONE',  ( 1.000000000000000000, 0.000000000000000000, 0.000000000000000000 ) ) ;
#78935=VECTOR ( 'NONE', #121907, 1000.000000000000000 ) ;
#78937=VECTOR ( 'NONE', #131587, 1000.000000000000227 ) ;
#78938=VECTOR ( 'NONE', #97181, 1000.000000000000227 ) ;
#78939=DIRECTION ( 'NONE',  ( 0.6830127018922180770, -0.6830127018922204085, -0.2588190451025213501 ) ) ;
#78940=ORIENTED_EDGE ( 'NONE', *, *, #136031, .T. ) ;
#78941=AXIS2_PLACEMENT_3D ( 'NONE', #5448, #117768, #41676 ) ;
#78942=CARTESIAN_POINT ( 'NONE',  ( -12.51168605928424249, 6.759292476615645917, 16.35960578974472313 ) ) ;
#78943=ORIENTED_EDGE ( 'NONE', *, *, #85655, .F. ) ;
#78946=CARTESIAN_POINT ( 'NONE',  ( -41.99451991528749062, 28.92564299267967343, 4.000000000000000000 ) ) ;
#78947=ORIENTED_EDGE ( 'NONE', *, *, #21103, .F. ) ;
#78948=CARTESIAN_POINT ( 'NONE',  ( -31.17183060077625001, 9.759292476615625489, 4.000000000000000000 ) ) ;
#78950=ORIENTED_EDGE ( 'NONE', *, *, #98504, .F. ) ;
#78951=VECTOR ( 'NONE', #61429, 1000.000000000000000 ) ;
#78952=ORIENTED_EDGE ( 'NONE', *, *, #136249, .F. ) ;
#78954=DIRECTION ( 'NONE',  ( -0.6830127018922181881, 0.6830127018922202975, -0.2588190451025214056 ) ) ;
#78955=CARTESIAN_POINT ( 'NONE',  ( -69.18398860626899705, 28.73617430169835529, 5.000000000000000000 ) ) ;
#78959=CARTESIAN_POINT ( 'NONE',  ( -29.99999999999979039, -19.44781430457063465, 5.000000000000000000 ) ) ;
#78960=VECTOR ( 'NONE', #48061, 1000.000000000000227 ) ;
#78961=CARTESIAN_POINT ( 'NONE',  ( 24.62910658713767731, 1.050808743928695277, 4.662926800793053772 ) ) ;
#78962=PLANE ( 'NONE',  #110692 ) ;
#78963=VECTOR ( 'NONE', #49780, 1000.000000000000000 ) ;
#78964=CARTESIAN_POINT ( 'NONE',  ( 12.29974487139158512, -27.71228299555214747, 4.000000000000000000 ) ) ;
#78965=CARTESIAN_POINT ( 'NONE',  ( 33.48921356237309510, -27.52281430457078670, 5.000000000000000000 ) ) ;
#78966=ORIENTED_EDGE ( 'NONE', *, *, #109956, .T. ) ;
#78967=AXIS2_PLACEMENT_3D ( 'NONE', #1622, #82620, #56086 ) ;
#78968=PLANE ( 'NONE',  #48098 ) ;
#78969=CARTESIAN_POINT ( 'NONE',  ( 34.45011844616451668, 1.516280811637481962, 5.000000000000000888 ) ) ;
#78970=CARTESIAN_POINT ( 'NONE',  ( 56.99451991528749062, 28.92564299267978001, 4.000000000000000000 ) ) ;
#78971=ORIENTED_EDGE ( 'NONE', *, *, #124678, .T. ) ;
#78973=ORIENTED_EDGE ( 'NONE', *, *, #103620, .F. ) ;
#78974=DIRECTION ( 'NONE',  ( 0.6830127018922180770, -0.6830127018922204085, -0.2588190451025213501 ) ) ;
#78975=ORIENTED_EDGE ( 'NONE', *, *, #28124, .T. ) ;
#78976=AXIS2_PLACEMENT_3D ( 'NONE', #51559, #95753, #141401 ) ;
#78977=EDGE_LOOP ( 'NONE', ( #102682, #109754, #142713, #133488 ) ) ;
#78978=DIRECTION ( 'NONE',  ( 0.000000000000000000, 0.000000000000000000, -1.000000000000000000 ) ) ;
#78979=LINE ( 'NONE', #135489, #64079 ) ;
#78980=DIRECTION ( 'NONE',  ( -0.3543493200069162685, -0.000000000000000000, -0.9351131265310288487 ) ) ;
#78981=FACE_OUTER_BOUND ( 'NONE', #8762, .T. ) ;
#78983=EDGE_LOOP ( 'NONE', ( #31940, #57608, #23876, #134909 ) ) ;
#78985=ORIENTED_EDGE ( 'NONE', *, *, #104390, .T. ) ;
#78986=LINE ( 'NONE', #12959, #46876 ) ;
#78987=VECTOR ( 'NONE', #1814, 1000.000000000000000 ) ;
#78989=EDGE_LOOP ( 'NONE', ( #101248, #138703, #4307, #100404 ) ) ;
#78992=DIRECTION ( 'NONE',  ( -0.7071067811865486830, 0.7071067811865464625, 0.000000000000000000 ) ) ;
#78993=ORIENTED_EDGE ( 'NONE', *, *, #37862, .T. ) ;
#78994=ORIENTED_EDGE ( 'NONE', *, *, #55880, .T. ) ;
#78995=ADVANCED_FACE ( 'NONE', ( #112908 ), #67280, .F. ) ;
#79000=LINE ( 'NONE', #12273, #56648 ) ;
#79003=ORIENTED_EDGE ( 'NONE', *, *, #19855, .F. ) ;
#79004=CARTESIAN_POINT ( 'NONE',  ( 3.183988606268992161, 28.73617430169789699, 5.000000000000000000 ) ) ;
#79005=EDGE_CURVE ( 'NONE', #137801, #117180, #1954, .T. ) ;
#79006=LINE ( 'NONE', #44227, #14221 ) ;
#79008=VECTOR ( 'NONE', #120078, 1000.000000000000000 ) ;
#79009=ADVANCED_FACE ( 'NONE', ( #112214 ), #70174, .F. ) ;
#79010=VERTEX_POINT ( 'NONE', #136801 ) ;
#79011=CARTESIAN_POINT ( 'NONE',  ( 14.48334561358944406, 22.22500000000000142, 4.500000000000000888 ) ) ;
#79012=VECTOR ( 'NONE', #85189, 1000.000000000000000 ) ;
#79013=CARTESIAN_POINT ( 'NONE',  ( 18.18398860626898994, 28.73617430169800002, 5.000000000000000000 ) ) ;
#79014=ORIENTED_EDGE ( 'NONE', *, *, #7544, .T. ) ;
#79015=EDGE_CURVE ( 'NONE', #82088, #122084, #78157, .T. ) ;
#79017=VERTEX_POINT ( 'NONE', #133951 ) ;
#79018=ORIENTED_EDGE ( 'NONE', *, *, #113032, .F. ) ;
#79019=ADVANCED_FACE ( 'NONE', ( #57849 ), #68034, .T. ) ;
#79020=EDGE_CURVE ( 'NONE', #87384, #127177, #36087, .T. ) ;
#79022=DIRECTION ( 'NONE',  ( 0.6830127018922181881, 0.6830127018922202975, -0.2588190451025214056 ) ) ;
#79023=VECTOR ( 'NONE', #17323, 1000.000000000000000 ) ;
#79024=ORIENTED_EDGE ( 'NONE', *, *, #104009, .F. ) ;
#79026=ORIENTED_EDGE ( 'NONE', *, *, #89164, .T. ) ;
#79030=DIRECTION ( 'NONE',  ( 0.7071067811865487940, 0.7071067811865463515, 0.000000000000000000 ) ) ;
#79031=DIRECTION ( 'NONE',  ( -0.7071067811865487940, 0.7071067811865463515, 0.000000000000000000 ) ) ;
#79032=FACE_OUTER_BOUND ( 'NONE', #104911, .T. ) ;
#79034=CARTESIAN_POINT ( 'NONE',  ( -36.18398860626899705, 28.73617430169812437, 5.000000000000000000 ) ) ;
#79035=EDGE_CURVE ( 'NONE', #5696, #18494, #49828, .T. ) ;
#79036=DIRECTION ( 'NONE',  ( 0.3543493200069162685, -0.000000000000000000, -0.9351131265310288487 ) ) ;
#79037=DIRECTION ( 'NONE',  ( 0.7071067811865487940, 0.7071067811865463515, 0.000000000000000000 ) ) ;
#79041=LINE ( 'NONE', #25320, #29669 ) ;
#79042=VECTOR ( 'NONE', #86286, 1000.000000000000000 ) ;
#79043=CARTESIAN_POINT ( 'NONE',  ( 0.000000000000000000, 0.000000000000000000, 5.000000000000000000 ) ) ;
#79044=CARTESIAN_POINT ( 'NONE',  ( -44.99451991528749772, 28.92564299267969474, 4.000000000000000000 ) ) ;
#79045=ORIENTED_EDGE ( 'NONE', *, *, #46378, .T. ) ;
#79046=ORIENTED_EDGE ( 'NONE', *, *, #51417, .T. ) ;
#79047=VECTOR ( 'NONE', #104774, 999.9999999999998863 ) ;
#79049=ADVANCED_FACE ( 'NONE', ( #29454 ), #28050, .F. ) ;
#79050=VECTOR ( 'NONE', #39689, 1000.000000000000227 ) ;
#79051=ORIENTED_EDGE ( 'NONE', *, *, #113793, .T. ) ;
#79052=VERTEX_POINT ( 'NONE', #51241 ) ;
#79055=CARTESIAN_POINT ( 'NONE',  ( -8.994519915287490619, 28.92564299267944250, 4.000000000000000000 ) ) ;
#79057=VECTOR ( 'NONE', #12992, 1000.000000000000000 ) ;
#79058=FACE_OUTER_BOUND ( 'NONE', #23306, .T. ) ;
#79059=VERTEX_POINT ( 'NONE', #73019 ) ;
#79060=FACE_OUTER_BOUND ( 'NONE', #59567, .T. ) ;
#79062=CARTESIAN_POINT ( 'NONE',  ( 9.668467411598506089, -18.74070752338409562, 20.73178291233843495 ) ) ;
#79063=LINE ( 'NONE', #2127, #88149 ) ;
#79067=CARTESIAN_POINT ( 'NONE',  ( 29.99999999999978684, -13.06887692260767686, 4.000000000000000000 ) ) ;
#79068=DIRECTION ( 'NONE',  ( 0.7071067811865487940, -0.7071067811865463515, 0.000000000000000000 ) ) ;
#79069=AXIS2_PLACEMENT_3D ( 'NONE', #123641, #24989, #133777 ) ;
#79070=DIRECTION ( 'NONE',  ( 0.7071067811865487940, 0.7071067811865463515, 0.000000000000000000 ) ) ;
#79072=CARTESIAN_POINT ( 'NONE',  ( -69.48921356237309510, -27.52281430457103895, 5.000000000000000000 ) ) ;
#79073=LINE ( 'NONE', #101484, #127949 ) ;
#79074=CARTESIAN_POINT ( 'NONE',  ( 34.42499999999998295, 8.977185695429312773, 5.000000000000000000 ) ) ;
#79076=ORIENTED_EDGE ( 'NONE', *, *, #49006, .F. ) ;
#79077=ORIENTED_EDGE ( 'NONE', *, *, #23989, .F. ) ;
#79079=VERTEX_POINT ( 'NONE', #37514 ) ;
#79081=CARTESIAN_POINT ( 'NONE',  ( -3.707013264293017141, -21.74070752338405299, 4.999753212805222446 ) ) ;
#79082=CARTESIAN_POINT ( 'NONE',  ( 24.32816939922335209, -21.74070752338406365, 4.000000000000000000 ) ) ;
#79083=LINE ( 'NONE', #123289, #90679 ) ;
#79084=DIRECTION ( 'NONE',  ( -0.6830127018922180770, -0.6830127018922204085, -0.2588190451025213501 ) ) ;
#79085=VECTOR ( 'NONE', #43429, 1000.000000000000000 ) ;
#79086=EDGE_CURVE ( 'NONE', #9095, #51427, #42519, .T. ) ;
#79087=VECTOR ( 'NONE', #118051, 1000.000000000000000 ) ;
#79089=ORIENTED_EDGE ( 'NONE', *, *, #96020, .F. ) ;
#79090=ADVANCED_FACE ( 'NONE', ( #109882 ), #121463, .T. ) ;
#79091=AXIS2_PLACEMENT_3D ( 'NONE', #82179, #103864, #137250 ) ;
#79092=EDGE_LOOP ( 'NONE', ( #28364, #60221, #66543, #38204 ) ) ;
#79093=VECTOR ( 'NONE', #20147, 1000.000000000000000 ) ;
#79094=DIRECTION ( 'NONE',  ( -0.6830127018922181881, 0.6830127018922202975, -0.2588190451025214056 ) ) ;
#79095=EDGE_CURVE ( 'NONE', #110079, #77841, #135975, .T. ) ;
#79096=ORIENTED_EDGE ( 'NONE', *, *, #12349, .F. ) ;
#79097=ORIENTED_EDGE ( 'NONE', *, *, #111270, .T. ) ;
#79098=ORIENTED_EDGE ( 'NONE', *, *, #140839, .F. ) ;
#79100=CARTESIAN_POINT ( 'NONE',  ( -5.671830600776427644, 8.259292476615630818, 4.000000000000000000 ) ) ;
#79102=EDGE_CURVE ( 'NONE', #82254, #116108, #19309, .T. ) ;
#79103=CARTESIAN_POINT ( 'NONE',  ( 18.48921356237309510, -27.52281430457068367, 5.000000000000000000 ) ) ;
#79104=ORIENTED_EDGE ( 'NONE', *, *, #69355, .F. ) ;
#79105=EDGE_CURVE ( 'NONE', #13957, #110495, #109167, .T. ) ;
#79106=CARTESIAN_POINT ( 'NONE',  ( -29.01088028653927964, -22.02621442084247505, 4.990779571109222879 ) ) ;
#79108=VERTEX_POINT ( 'NONE', #76571 ) ;
#79110=EDGE_LOOP ( 'NONE', ( #131450, #50040, #139428, #54162 ) ) ;
#79112=DIRECTION ( 'NONE',  ( -0.7071067811865486830, -0.7071067811865464625, 0.000000000000000000 ) ) ;
#79114=VERTEX_POINT ( 'NONE', #53357 ) ;
#79115=CARTESIAN_POINT ( 'NONE',  ( -6.489213562373093325, -27.52281430457059841, 5.000000000000000000 ) ) ;
#79117=VECTOR ( 'NONE', #39963, 999.9999999999998863 ) ;
#79118=CARTESIAN_POINT ( 'NONE',  ( 3.328169399223508851, 17.25929247661553489, 4.000000000000000000 ) ) ;
#79119=DIRECTION ( 'NONE',  ( 0.7071067811865486830, -0.7071067811865464625, -0.000000000000000000 ) ) ;
#79120=ADVANCED_FACE ( 'NONE', ( #98308 ), #97570, .T. ) ;
#79121=FACE_BOUND ( 'NONE', #73390, .T. ) ;
#79122=ORIENTED_EDGE ( 'NONE', *, *, #91985, .F. ) ;
#79125=LINE ( 'NONE', #23996, #14325 ) ;
#79126=VERTEX_POINT ( 'NONE', #9850 ) ;
#79127=DIRECTION ( 'NONE',  ( 1.000000000000000000, 0.000000000000000000, 0.000000000000000000 ) ) ;
#79128=VERTEX_POINT ( 'NONE', #41059 ) ;
#79129=VERTEX_POINT ( 'NONE', #8387 ) ;
#79130=AXIS2_PLACEMENT_3D ( 'NONE', #28371, #5137, #29765 ) ;
#79131=EDGE_LOOP ( 'NONE', ( #59779, #132002, #38514, #5144 ) ) ;
#79134=EDGE_LOOP ( 'NONE', ( #8926, #10793, #59246, #48003 ) ) ;
#79135=LINE ( 'NONE', #80545, #141328 ) ;
#79136=ADVANCED_FACE ( 'NONE', ( #54119 ), #31620, .F. ) ;
#79137=CARTESIAN_POINT ( 'NONE',  ( -33.18398860626899705, 28.73617430169810305, 5.000000000000000000 ) ) ;
#79140=VECTOR ( 'NONE', #21556, 1000.000000000000000 ) ;
#79141=VECTOR ( 'NONE', #128355, 1000.000000000000000 ) ;
#79142=EDGE_CURVE ( 'NONE', #97043, #62248, #10549, .T. ) ;
#79143=AXIS2_PLACEMENT_3D ( 'NONE', #41475, #108137, #141524 ) ;
#79144=AXIS2_PLACEMENT_3D ( 'NONE', #111326, #12010, #56298 ) ;
#79145=EDGE_CURVE ( 'NONE', #81561, #125811, #96827, .T. ) ;
#79146=DIRECTION ( 'NONE',  ( -0.000000000000000000, 0.3543493200069153248, 0.9351131265310292928 ) ) ;
#79147=CARTESIAN_POINT ( 'NONE',  ( -16.41009064519821337, 9.759292476615618384, 11.28811694763775009 ) ) ;
#79149=DIRECTION ( 'NONE',  ( -0.6830127018922181881, 0.6830127018922202975, -0.2588190451025214056 ) ) ;
#79150=ORIENTED_EDGE ( 'NONE', *, *, #81757, .F. ) ;
#79151=ORIENTED_EDGE ( 'NONE', *, *, #116494, .F. ) ;
#79152=VECTOR ( 'NONE', #117820, 1000.000000000000000 ) ;
#79155=AXIS2_PLACEMENT_3D ( 'NONE', #32306, #11949, #56236 ) ;
#79156=EDGE_LOOP ( 'NONE', ( #95232, #108148, #34507, #77775 ) ) ;
#79158=EDGE_LOOP ( 'NONE', ( #86906, #120013, #102426, #55133 ) ) ;
#79160=ORIENTED_EDGE ( 'NONE', *, *, #2178, .T. ) ;
#79162=EDGE_CURVE ( 'NONE', #116810, #129956, #63565, .T. ) ;
#79164=EDGE_LOOP ( 'NONE', ( #50889, #45130, #117800, #99921, #137794 ) ) ;
#79166=DIRECTION ( 'NONE',  ( -0.6830127018922181881, 0.6830127018922202975, -0.2588190451025214056 ) ) ;
#79167=LINE ( 'NONE', #14578, #125470 ) ;
#79170=ORIENTED_EDGE ( 'NONE', *, *, #133584, .T. ) ;
#79172=CARTESIAN_POINT ( 'NONE',  ( -11.99999999999991296, 5.966399257802200040, 5.000000000000000000 ) ) ;
#79173=CARTESIAN_POINT ( 'NONE',  ( -34.92500000000001137, 22.22500000000000142, 4.000000000000000000 ) ) ;
#79174=CARTESIAN_POINT ( 'NONE',  ( 12.41161490594822503, 22.22500000000000142, 4.777194822843815913 ) ) ;
#79175=VERTEX_POINT ( 'NONE', #74423 ) ;
#79176=CARTESIAN_POINT ( 'NONE',  ( 8.293876922607989144, 22.22500000000000142, 4.000000000000000000 ) ) ;
#79177=DIRECTION ( 'NONE',  ( 0.7071067811865487940, 0.7071067811865463515, 0.000000000000000000 ) ) ;
#79178=ORIENTED_EDGE ( 'NONE', *, *, #16812, .F. ) ;
#79179=DIRECTION ( 'NONE',  ( -0.7071067811865486830, -0.7071067811865464625, 0.000000000000000000 ) ) ;
#79180=VERTEX_POINT ( 'NONE', #98992 ) ;
#79182=PLANE ( 'NONE',  #109415 ) ;
#79185=AXIS2_PLACEMENT_3D ( 'NONE', #66455, #44738, #54176 ) ;
#79186=DIRECTION ( 'NONE',  ( 1.000000000000000000, 0.000000000000000000, 0.000000000000000000 ) ) ;
#79187=VECTOR ( 'NONE', #54660, 1000.000000000000227 ) ;
#79188=LINE ( 'NONE', #24058, #132121 ) ;
#79189=CARTESIAN_POINT ( 'NONE',  ( -12.18398860626900060, 28.73617430169795739, 5.000000000000000000 ) ) ;
#79190=ORIENTED_EDGE ( 'NONE', *, *, #45463, .T. ) ;
#79191=VECTOR ( 'NONE', #115696, 1000.000000000000000 ) ;
#79192=DIRECTION ( 'NONE',  ( -0.7071067811865486830, -0.7071067811865464625, 0.000000000000000000 ) ) ;
#79193=EDGE_CURVE ( 'NONE', #95370, #92431, #132392, .T. ) ;
#79194=ORIENTED_EDGE ( 'NONE', *, *, #48167, .F. ) ;
#79195=DIRECTION ( 'NONE',  ( 0.7071067811865487940, 0.7071067811865463515, 0.000000000000000000 ) ) ;
#79196=DIRECTION ( 'NONE',  ( 0.000000000000000000, 0.000000000000000000, -1.000000000000000000 ) ) ;
#79197=ORIENTED_EDGE ( 'NONE', *, *, #109440, .F. ) ;
#79198=EDGE_CURVE ( 'NONE', #99716, #88687, #81401, .T. ) ;
#79199=ADVANCED_FACE ( 'NONE', ( #122167 ), #112736, .F. ) ;
#79200=ORIENTED_EDGE ( 'NONE', *, *, #41852, .F. ) ;
#79201=LINE ( 'NONE', #35697, #135263 ) ;
#79202=LINE ( 'NONE', #24069, #25106 ) ;
#79203=VECTOR ( 'NONE', #124917, 1000.000000000000000 ) ;
#79204=ORIENTED_EDGE ( 'NONE', *, *, #121863, .T. ) ;
#79205=CARTESIAN_POINT ( 'NONE',  ( 30.18398860626900060, 28.73617430169808173, 5.000000000000000000 ) ) ;
#79206=EDGE_CURVE ( 'NONE', #47599, #50105, #89555, .T. ) ;
#79208=CARTESIAN_POINT ( 'NONE',  ( 39.18398860626899705, 28.73617430169814568, 5.000000000000000000 ) ) ;
#79209=FACE_OUTER_BOUND ( 'NONE', #51498, .T. ) ;
#79210=EDGE_CURVE ( 'NONE', #40163, #79781, #56966, .T. ) ;
#79212=FACE_OUTER_BOUND ( 'NONE', #26929, .T. ) ;
#79214=FACE_OUTER_BOUND ( 'NONE', #40104, .T. ) ;
#79215=AXIS2_PLACEMENT_3D ( 'NONE', #65892, #110051, #142011 ) ;
#79216=DIRECTION ( 'NONE',  ( 0.3543493200069162685, -0.000000000000000000, -0.9351131265310288487 ) ) ;
#79217=DIRECTION ( 'NONE',  ( -0.7071067811865486830, -0.7071067811865464625, -0.000000000000000000 ) ) ;
#79218=AXIS2_PLACEMENT_3D ( 'NONE', #133924, #24440, #10678 ) ;
#79219=FACE_OUTER_BOUND ( 'NONE', #56969, .T. ) ;
#79220=ADVANCED_FACE ( 'NONE', ( #80847 ), #88872, .T. ) ;
#79221=CARTESIAN_POINT ( 'NONE',  ( -24.48921356237309510, -27.52281430457072631, 5.000000000000000000 ) ) ;
#79222=EDGE_LOOP ( 'NONE', ( #55074, #25810, #39620, #69034 ) ) ;
#79223=ORIENTED_EDGE ( 'NONE', *, *, #27965, .F. ) ;
#79224=VERTEX_POINT ( 'NONE', #35211 ) ;
#79226=EDGE_CURVE ( 'NONE', #116321, #71945, #1784, .T. ) ;
#79227=ORIENTED_EDGE ( 'NONE', *, *, #87884, .T. ) ;
#79229=EDGE_LOOP ( 'NONE', ( #83753, #24270, #105655, #56917 ) ) ;
#79232=DIRECTION ( 'NONE',  ( -0.000000000000000000, 0.000000000000000000, 1.000000000000000000 ) ) ;
#79233=ORIENTED_EDGE ( 'NONE', *, *, #29927, .F. ) ;
#79234=CARTESIAN_POINT ( 'NONE',  ( -17.99999999999987566, 19.93112307739198386, 4.000000000000000000 ) ) ;
#79236=EDGE_CURVE ( 'NONE', #68198, #14802, #90262, .T. ) ;
#79237=DIRECTION ( 'NONE',  ( 0.3543493200069162685, -0.000000000000000000, -0.9351131265310288487 ) ) ;
#79238=PLANE ( 'NONE',  #32536 ) ;
#79240=ORIENTED_EDGE ( 'NONE', *, *, #77418, .T. ) ;
#79243=CARTESIAN_POINT ( 'NONE',  ( 6.183988606268994381, 28.73617430169791476, 5.000000000000000000 ) ) ;
#79248=CARTESIAN_POINT ( 'NONE',  ( -17.67183060077634593, -21.74070752338406010, 4.000000000000000000 ) ) ;
#79249=DIRECTION ( 'NONE',  ( -0.000000000000000000, 0.3543493200069153248, 0.9351131265310292928 ) ) ;
#79251=CARTESIAN_POINT ( 'NONE',  ( -30.48921356237309510, -27.52281430457076894, 5.000000000000000000 ) ) ;
#79252=LINE ( 'NONE', #87931, #11323 ) ;
#79253=VERTEX_POINT ( 'NONE', #35926 ) ;
#79256=DIRECTION ( 'NONE',  ( -0.000000000000000000, 0.000000000000000000, 1.000000000000000000 ) ) ;
#79258=VECTOR ( 'NONE', #87185, 1000.000000000000000 ) ;
#79260=VECTOR ( 'NONE', #41245, 1000.000000000000000 ) ;
#79262=( BOUNDED_CURVE ( )  B_SPLINE_CURVE ( 3, ( #139351, #30567, #105941, #63224 ),
 .UNSPECIFIED., .F., .F. ) 
 B_SPLINE_CURVE_WITH_KNOTS ( ( 4, 4 ),
 ( 5.143245962375972091, 6.645403452391247079 ),
 .UNSPECIFIED. ) 
 CURVE ( )  GEOMETRIC_REPRESENTATION_ITEM ( )  RATIONAL_B_SPLINE_CURVE ( ( 1.000000000000000000, 0.8206354192515254997, 0.8206354192515254997, 1.000000000000000000 ) ) 
 REPRESENTATION_ITEM ( '' )  );
#79263=LINE ( 'NONE', #89375, #139484 ) ;
#79264=VECTOR ( 'NONE', #107800, 1000.000000000000000 ) ;
#79267=ORIENTED_EDGE ( 'NONE', *, *, #124702, .F. ) ;
#79268=ADVANCED_FACE ( 'NONE', ( #134510 ), #56272, .F. ) ;
#79269=DIRECTION ( 'NONE',  ( -0.7071067811865486830, -0.7071067811865464625, 0.000000000000000000 ) ) ;
#79270=EDGE_LOOP ( 'NONE', ( #126607, #67283, #93189 ) ) ;
#79272=AXIS2_PLACEMENT_3D ( 'NONE', #92921, #26250, #2306 ) ;
#79274=CARTESIAN_POINT ( 'NONE',  ( 18.10180811604841011, 9.068207373850700748, 5.000000000000000000 ) ) ;
#79276=EDGE_CURVE ( 'NONE', #20488, #48699, #91016, .T. ) ;
#79277=DIRECTION ( 'NONE',  ( -0.6830127018922180770, -0.6830127018922204085, -0.2588190451025213501 ) ) ;
#79278=ORIENTED_EDGE ( 'NONE', *, *, #130605, .F. ) ;
#79279=CARTESIAN_POINT ( 'NONE',  ( -24.65671000166197757, 3.759292476615681888, 13.27625715073259904 ) ) ;
#79280=ORIENTED_EDGE ( 'NONE', *, *, #76782, .T. ) ;
#79282=LINE ( 'NONE', #34299, #92480 ) ;
#79284=DIRECTION ( 'NONE',  ( -0.7071067811865487940, 0.7071067811865463515, -0.000000000000000000 ) ) ;
#79286=EDGE_LOOP ( 'NONE', ( #88643, #108254, #73247, #113562 ) ) ;
#79287=DIRECTION ( 'NONE',  ( 0.7071067811865486830, -0.7071067811865464625, -0.000000000000000000 ) ) ;
#79289=CARTESIAN_POINT ( 'NONE',  ( -54.18398860626899705, 28.73617430169825226, 5.000000000000000000 ) ) ;
#79291=PLANE ( 'NONE',  #80212 ) ;
#79292=DIRECTION ( 'NONE',  ( -0.7071067811865487940, 0.7071067811865463515, 0.000000000000000000 ) ) ;
#79293=ORIENTED_EDGE ( 'NONE', *, *, #99351, .T. ) ;
#79294=ORIENTED_EDGE ( 'NONE', *, *, #8699, .F. ) ;
#79295=DIRECTION ( 'NONE',  ( -0.3543493200069162685, -0.000000000000000000, -0.9351131265310288487 ) ) ;
#79296=ORIENTED_EDGE ( 'NONE', *, *, #122470, .F. ) ;
#79297=VECTOR ( 'NONE', #107617, 999.9999999999998863 ) ;
#79298=VECTOR ( 'NONE', #78543, 1000.000000000000000 ) ;
#79301=VECTOR ( 'NONE', #87514, 1000.000000000000000 ) ;
#79302=CARTESIAN_POINT ( 'NONE',  ( 0.000000000000000000, 0.000000000000000000, 5.000000000000000000 ) ) ;
#79303=DIRECTION ( 'NONE',  ( -0.7071067811865487940, 0.7071067811865463515, 0.000000000000000000 ) ) ;
#79304=LINE ( 'NONE', #74453, #124952 ) ;
#79305=VECTOR ( 'NONE', #10191, 999.9999999999998863 ) ;
#79306=DIRECTION ( 'NONE',  ( 0.6830127018922181881, 0.6830127018922202975, -0.2588190451025214056 ) ) ;
#79307=EDGE_CURVE ( 'NONE', #967, #92118, #25724, .T. ) ;
#79308=FACE_BOUND ( 'NONE', #63219, .T. ) ;
#79309=CARTESIAN_POINT ( 'NONE',  ( 44.99451991528749772, 28.92564299267969474, 4.000000000000000000 ) ) ;
#79310=EDGE_CURVE ( 'NONE', #46586, #305, #23585, .T. ) ;
#79311=CARTESIAN_POINT ( 'NONE',  ( 9.489213562373095101, -27.52281430457062328, 5.000000000000000000 ) ) ;
#79312=DIRECTION ( 'NONE',  ( 0.6830127018922181881, 0.6830127018922202975, -0.2588190451025214056 ) ) ;
#79317=EDGE_LOOP ( 'NONE', ( #68830, #52312, #4455, #7160 ) ) ;
#79319=ORIENTED_EDGE ( 'NONE', *, *, #136579, .T. ) ;
#79320=CARTESIAN_POINT ( 'NONE',  ( -39.48921356237310221, -27.52281430457082934, 5.000000000000000000 ) ) ;
#79321=EDGE_CURVE ( 'NONE', #14462, #11390, #33780, .T. ) ;
#79323=ORIENTED_EDGE ( 'NONE', *, *, #26345, .T. ) ;
#79324=LINE ( 'NONE', #247, #111543 ) ;
#79325=VECTOR ( 'NONE', #5355, 1000.000000000000000 ) ;
#79326=EDGE_CURVE ( 'NONE', #101708, #56732, #45381, .T. ) ;
#79328=EDGE_CURVE ( 'NONE', #99670, #6450, #126453, .T. ) ;
#79329=CARTESIAN_POINT ( 'NONE',  ( -11.99451991528749417, 28.92564299267946382, 4.000000000000000000 ) ) ;
#79330=CARTESIAN_POINT ( 'NONE',  ( 42.29974487139158157, -27.71228299555235708, 4.000000000000000000 ) ) ;
#79331=LINE ( 'NONE', #68442, #45844 ) ;
#79332=DIRECTION ( 'NONE',  ( -0.6830127018922181881, 0.6830127018922202975, -0.2588190451025214056 ) ) ;
#79333=LINE ( 'NONE', #15409, #36990 ) ;
#79335=VECTOR ( 'NONE', #115292, 1000.000000000000000 ) ;
#79336=VECTOR ( 'NONE', #17352, 1000.000000000000000 ) ;
#79337=ORIENTED_EDGE ( 'NONE', *, *, #55483, .T. ) ;
#79338=CARTESIAN_POINT ( 'NONE',  ( 1.828169399223519953, 0.7592924766157069794, 4.000000000000000000 ) ) ;
#79339=CARTESIAN_POINT ( 'NONE',  ( -29.67183060077625711, -12.74070752338414891, 4.000000000000000000 ) ) ;
#79340=ORIENTED_EDGE ( 'NONE', *, *, #9108, .F. ) ;
#79341=VERTEX_POINT ( 'NONE', #51063 ) ;
#79342=ORIENTED_EDGE ( 'NONE', *, *, #34544, .F. ) ;
#79343=EDGE_CURVE ( 'NONE', #77443, #91920, #38751, .T. ) ;
#79344=CARTESIAN_POINT ( 'NONE',  ( 39.18398860626899705, 28.73617430169814568, 5.000000000000000000 ) ) ;
#79345=AXIS2_PLACEMENT_3D ( 'NONE', #35738, #82092, #24809 ) ;
#79347=DIRECTION ( 'NONE',  ( 0.7071067811865487940, 0.7071067811865463515, 0.000000000000000000 ) ) ;
#79350=CARTESIAN_POINT ( 'NONE',  ( 0.000000000000000000, 9.631307414974321190, -9.079085613539540134 ) ) ;
#79351=VERTEX_POINT ( 'NONE', #40214 ) ;
#79352=CARTESIAN_POINT ( 'NONE',  ( 0.000000000000000000, 0.000000000000000000, 5.000000000000000000 ) ) ;
#79353=DIRECTION ( 'NONE',  ( -0.000000000000000000, 0.3543493200069153248, 0.9351131265310292928 ) ) ;
#79354=PLANE ( 'NONE',  #40567 ) ;
#79355=VECTOR ( 'NONE', #66522, 999.9999999999998863 ) ;
#79356=VECTOR ( 'NONE', #105345, 1000.000000000000000 ) ;
#79357=DIRECTION ( 'NONE',  ( 0.3543493200069162685, -0.000000000000000000, -0.9351131265310288487 ) ) ;
#79358=ORIENTED_EDGE ( 'NONE', *, *, #71746, .F. ) ;
#79359=AXIS2_PLACEMENT_3D ( 'NONE', #24494, #68748, #112932 ) ;
#79360=ORIENTED_EDGE ( 'NONE', *, *, #70278, .F. ) ;
#79361=LINE ( 'NONE', #22743, #72796 ) ;
#79363=VECTOR ( 'NONE', #48270, 999.9999999999998863 ) ;
#79364=LINE ( 'NONE', #24918, #79506 ) ;
#79365=VECTOR ( 'NONE', #21682, 999.9999999999998863 ) ;
#79366=VERTEX_POINT ( 'NONE', #138795 ) ;
#79367=CARTESIAN_POINT ( 'NONE',  ( 25.49999999999982947, 1.030536316426536203, -5.498701923753857024 ) ) ;
#79370=PLANE ( 'NONE',  #116522 ) ;
#79371=VECTOR ( 'NONE', #142346, 1000.000000000000227 ) ;
#79372=VECTOR ( 'NONE', #125929, 1000.000000000000000 ) ;
#79374=CARTESIAN_POINT ( 'NONE',  ( 17.70025512860841488, -27.71228299555193786, 4.000000000000000000 ) ) ;
#79375=DIRECTION ( 'NONE',  ( -0.7071067811865487940, 0.7071067811865463515, 0.000000000000000000 ) ) ;
#79376=LINE ( 'NONE', #81498, #3371 ) ;
#79377=LINE ( 'NONE', #22756, #36746 ) ;
#79378=VERTEX_POINT ( 'NONE', #50349 ) ;
#79379=EDGE_LOOP ( 'NONE', ( #82578, #36464, #75505, #129323 ) ) ;
#79380=CARTESIAN_POINT ( 'NONE',  ( 34.82816939922329880, 21.75929247661549581, 4.000000000000000000 ) ) ;
#79381=LINE ( 'NONE', #58352, #37782 ) ;
#79383=DIRECTION ( 'NONE',  ( -0.000000000000000000, 0.3543493200069153248, 0.9351131265310292928 ) ) ;
#79384=ADVANCED_FACE ( 'NONE', ( #48201 ), #29290, .F. ) ;
#79385=ORIENTED_EDGE ( 'NONE', *, *, #47539, .T. ) ;
#79387=CARTESIAN_POINT ( 'NONE',  ( -3.498163485139541784, -17.24070752338410628, 8.407044977365233152 ) ) ;
#79388=DIRECTION ( 'NONE',  ( -0.7071067811865486830, -0.7071067811865464625, -0.000000000000000000 ) ) ;
#79390=ADVANCED_FACE ( 'NONE', ( #104712 ), #28605, .F. ) ;
#79391=EDGE_CURVE ( 'NONE', #482, #75148, #105414, .T. ) ;
#79392=ORIENTED_EDGE ( 'NONE', *, *, #86165, .F. ) ;
#79393=CARTESIAN_POINT ( 'NONE',  ( -20.99451991528748707, 28.92564299267952777, 4.000000000000000000 ) ) ;
#79394=EDGE_CURVE ( 'NONE', #15499, #21301, #48930, .T. ) ;
#79397=EDGE_CURVE ( 'NONE', #104700, #122337, #73532, .T. ) ;
#79400=DIRECTION ( 'NONE',  ( -0.7071067811865486830, 0.7071067811865464625, 0.000000000000000000 ) ) ;
#79402=DIRECTION ( 'NONE',  ( 0.6830127018922180770, -0.6830127018922204085, -0.2588190451025213501 ) ) ;
#79403=AXIS2_PLACEMENT_3D ( 'NONE', #87350, #131566, #32254 ) ;
#79405=EDGE_CURVE ( 'NONE', #79734, #21635, #139815, .T. ) ;
#79409=CARTESIAN_POINT ( 'NONE',  ( -35.99451991528749772, 28.92564299267963079, 4.000000000000000000 ) ) ;
#79411=LINE ( 'NONE', #48881, #141029 ) ;
#79412=CARTESIAN_POINT ( 'NONE',  ( 14.70025512860841133, -27.71228299555195917, 4.000000000000000000 ) ) ;
#79413=EDGE_CURVE ( 'NONE', #26486, #23088, #39482, .T. ) ;
#79416=LINE ( 'NONE', #33042, #115782 ) ;
#79417=DIRECTION ( 'NONE',  ( 0.3543493200069162685, -0.000000000000000000, -0.9351131265310288487 ) ) ;
#79419=ORIENTED_EDGE ( 'NONE', *, *, #86028, .T. ) ;
#79420=CARTESIAN_POINT ( 'NONE',  ( 81.18398860626899705, 28.73617430169844056, 5.000000000000000000 ) ) ;
#79422=CARTESIAN_POINT ( 'NONE',  ( -13.63753812416088707, 22.22500000000000142, 4.000000000000000000 ) ) ;
#79427=LINE ( 'NONE', #123625, #129330 ) ;
#79428=ORIENTED_EDGE ( 'NONE', *, *, #5463, .T. ) ;
#79429=( BOUNDED_CURVE ( )  B_SPLINE_CURVE ( 3, ( #13105, #87125, #65403, #55214 ),
 .UNSPECIFIED., .F., .T. ) 
 B_SPLINE_CURVE_WITH_KNOTS ( ( 4, 4 ),
 ( 2.779374508378133601, 4.199602562396783867 ),
 .UNSPECIFIED. ) 
 CURVE ( )  GEOMETRIC_REPRESENTATION_ITEM ( )  RATIONAL_B_SPLINE_CURVE ( ( 1.000000000000000000, 0.8388583629366745953, 0.8388583629366745953, 1.000000000000000000 ) ) 
 REPRESENTATION_ITEM ( '' )  );
#79431=CARTESIAN_POINT ( 'NONE',  ( 11.81601139373100651, 28.73617430169779041, 5.000000000000000000 ) ) ;
#79432=CARTESIAN_POINT ( 'NONE',  ( 29.99451991528749417, 28.92564299267958816, 4.000000000000000000 ) ) ;
#79433=CARTESIAN_POINT ( 'NONE',  ( 48.18398860626899705, 28.73617430169820608, 5.000000000000000000 ) ) ;
#79434=VECTOR ( 'NONE', #124376, 999.9999999999998863 ) ;
#79435=EDGE_CURVE ( 'NONE', #66820, #5794, #17681, .T. ) ;
#79436=AXIS2_PLACEMENT_3D ( 'NONE', #143204, #43905, #12673 ) ;
#79438=PLANE ( 'NONE',  #116262 ) ;
#79439=LINE ( 'NONE', #24981, #99892 ) ;
#79442=ORIENTED_EDGE ( 'NONE', *, *, #73155, .T. ) ;
#79445=CARTESIAN_POINT ( 'NONE',  ( 38.99451991528749062, 28.92564299267965211, 4.000000000000000000 ) ) ;
#79447=CARTESIAN_POINT ( 'NONE',  ( -42.48921356237308800, -27.52281430457085065, 5.000000000000000000 ) ) ;
#79448=LINE ( 'NONE', #24299, #25636 ) ;
#79450=VERTEX_POINT ( 'NONE', #106110 ) ;
#79451=DIRECTION ( 'NONE',  ( -0.6830127018922180770, -0.6830127018922204085, -0.2588190451025213501 ) ) ;
#79452=CARTESIAN_POINT ( 'NONE',  ( 0.000000000000000000, 0.000000000000000000, 5.000000000000000000 ) ) ;
#79456=ORIENTED_EDGE ( 'NONE', *, *, #29215, .T. ) ;
#79457=EDGE_CURVE ( 'NONE', #35917, #68848, #17001, .T. ) ;
#79458=ORIENTED_EDGE ( 'NONE', *, *, #91433, .T. ) ;
#79460=EDGE_LOOP ( 'NONE', ( #79706, #15344, #79760, #89195 ) ) ;
#79461=LINE ( 'NONE', #24314, #121634 ) ;
#79462=CARTESIAN_POINT ( 'NONE',  ( 20.99999999999986144, 14.96639925780210767, 5.000000000000000000 ) ) ;
#79463=LINE ( 'NONE', #133110, #78058 ) ;
#79464=ADVANCED_FACE ( 'NONE', ( #26450 ), #139531, .F. ) ;
#79465=CARTESIAN_POINT ( 'NONE',  ( 15.77004279457781877, 21.73644205237997085, 5.000000000000000888 ) ) ;
#79467=ORIENTED_EDGE ( 'NONE', *, *, #3500, .F. ) ;
#79468=ORIENTED_EDGE ( 'NONE', *, *, #115211, .T. ) ;
#79469=AXIS2_PLACEMENT_3D ( 'NONE', #65280, #88451, #55097 ) ;
#79470=CARTESIAN_POINT ( 'NONE',  ( -32.29289321881322650, -12.74070752338415602, 5.000000000000000000 ) ) ;
#79472=AXIS2_PLACEMENT_3D ( 'NONE', #9569, #117608, #95887 ) ;
#79473=VECTOR ( 'NONE', #116898, 1000.000000000000000 ) ;
#79474=EDGE_LOOP ( 'NONE', ( #48138, #84498, #19173, #88737 ) ) ;
#79475=EDGE_CURVE ( 'NONE', #132213, #80270, #84421, .T. ) ;
#79476=CARTESIAN_POINT ( 'NONE',  ( 9.489213562373095101, -27.52281430457062328, 5.000000000000000000 ) ) ;
#79477=VECTOR ( 'NONE', #84669, 1000.000000000000000 ) ;
#79478=LINE ( 'NONE', #135260, #27081 ) ;
#79479=DIRECTION ( 'NONE',  ( -0.7071067811865486830, -0.7071067811865464625, 0.000000000000000000 ) ) ;
#79481=VERTEX_POINT ( 'NONE', #53941 ) ;
#79483=FACE_BOUND ( 'NONE', #12456, .T. ) ;
#79484=LINE ( 'NONE', #102627, #124338 ) ;
#79485=PLANE ( 'NONE',  #113777 ) ;
#79486=CARTESIAN_POINT ( 'NONE',  ( -18.79289321881332597, -8.240707523384195099, 5.000000000000000000 ) ) ;
#79487=FACE_OUTER_BOUND ( 'NONE', #76112, .T. ) ;
#79488=CARTESIAN_POINT ( 'NONE',  ( -71.99451991528749772, 28.92564299267988304, 4.000000000000000000 ) ) ;
#79490=ORIENTED_EDGE ( 'NONE', *, *, #47306, .F. ) ;
#79491=AXIS2_PLACEMENT_3D ( 'NONE', #5856, #38523, #135010 ) ;
#79492=VERTEX_POINT ( 'NONE', #130051 ) ;
#79494=ORIENTED_EDGE ( 'NONE', *, *, #39045, .T. ) ;
#79495=FACE_OUTER_BOUND ( 'NONE', #136209, .T. ) ;
#79496=EDGE_CURVE ( 'NONE', #110666, #45152, #31450, .T. ) ;
#79497=ORIENTED_EDGE ( 'NONE', *, *, #121287, .F. ) ;
#79498=FACE_OUTER_BOUND ( 'NONE', #111997, .T. ) ;
#79499=AXIS2_PLACEMENT_3D ( 'NONE', #124942, #101764, #112646 ) ;
#79500=DIRECTION ( 'NONE',  ( 1.000000000000000000, 0.000000000000000000, 0.000000000000000000 ) ) ;
#79501=DIRECTION ( 'NONE',  ( 0.000000000000000000, 0.3543493200069153248, 0.9351131265310291818 ) ) ;
#79502=ORIENTED_EDGE ( 'NONE', *, *, #39513, .F. ) ;
#79503=DIRECTION ( 'NONE',  ( -0.000000000000000000, -0.3543493200069152693, 0.9351131265310292928 ) ) ;
#79505=PLANE ( 'NONE',  #40828 ) ;
#79506=VECTOR ( 'NONE', #47452, 1000.000000000000000 ) ;
#79509=CARTESIAN_POINT ( 'NONE',  ( -26.90332935812578086, -2.240707523384264377, 15.26439735382746221 ) ) ;
#79510=DIRECTION ( 'NONE',  ( -0.7071067811865486830, -0.7071067811865464625, -0.000000000000000000 ) ) ;
#79511=ORIENTED_EDGE ( 'NONE', *, *, #117361, .T. ) ;
#79513=PLANE ( 'NONE',  #46569 ) ;
#79514=VECTOR ( 'NONE', #134435, 999.9999999999998863 ) ;
#79515=ORIENTED_EDGE ( 'NONE', *, *, #35035, .T. ) ;
#79518=EDGE_CURVE ( 'NONE', #141782, #80772, #143056, .T. ) ;
#79521=VERTEX_POINT ( 'NONE', #21285 ) ;
#79523=FACE_OUTER_BOUND ( 'NONE', #38674, .T. ) ;
#79524=VECTOR ( 'NONE', #43856, 1000.000000000000000 ) ;
#79527=CARTESIAN_POINT ( 'NONE',  ( 28.49999999999981171, -16.91253812416058011, 4.000000000000000000 ) ) ;
#79528=EDGE_LOOP ( 'NONE', ( #21513, #68043, #12217, #103838 ) ) ;
#79529=CARTESIAN_POINT ( 'NONE',  ( -29.99999999999978328, 5.966399257802205369, 5.000000000000000000 ) ) ;
#79530=ORIENTED_EDGE ( 'NONE', *, *, #95559, .T. ) ;
#79531=PLANE ( 'NONE',  #76561 ) ;
#79533=PLANE ( 'NONE',  #111954 ) ;
#79535=EDGE_CURVE ( 'NONE', #118679, #5639, #95971, .T. ) ;
#79536=DIRECTION ( 'NONE',  ( -0.3543493200069163240, -0.000000000000000000, -0.9351131265310288487 ) ) ;
#79537=CARTESIAN_POINT ( 'NONE',  ( -6.461603553705668190, -9.740707523384180888, 17.74957260769609135 ) ) ;
#79539=ORIENTED_EDGE ( 'NONE', *, *, #98639, .T. ) ;
#79540=CARTESIAN_POINT ( 'NONE',  ( -36.48921356237310221, -27.52281430457080802, 5.000000000000000000 ) ) ;
#79542=ORIENTED_EDGE ( 'NONE', *, *, #65542, .F. ) ;
#79543=VERTEX_POINT ( 'NONE', #19136 ) ;
#79544=PLANE ( 'NONE',  #5369 ) ;
#79545=VECTOR ( 'NONE', #61296, 1000.000000000000000 ) ;
#79547=CARTESIAN_POINT ( 'NONE',  ( -9.183988606268997046, 28.73617430169793607, 5.000000000000000000 ) ) ;
#79548=DIRECTION ( 'NONE',  ( -0.000000000000000000, -0.3543493200069152693, 0.9351131265310292928 ) ) ;
#79549=FACE_OUTER_BOUND ( 'NONE', #71552, .T. ) ;
#79550=VECTOR ( 'NONE', #85259, 1000.000000000000227 ) ;
#79551=ORIENTED_EDGE ( 'NONE', *, *, #75665, .F. ) ;
#79552=CARTESIAN_POINT ( 'NONE',  ( 21.48921356237309155, -27.52281430457070499, 5.000000000000000000 ) ) ;
#79554=DIRECTION ( 'NONE',  ( 0.7071067811865487940, 0.7071067811865463515, 0.000000000000000000 ) ) ;
#79555=EDGE_CURVE ( 'NONE', #88426, #142286, #9671, .T. ) ;
#79556=DIRECTION ( 'NONE',  ( 1.000000000000000000, 0.000000000000000000, 0.000000000000000000 ) ) ;
#79558=ORIENTED_EDGE ( 'NONE', *, *, #13265, .F. ) ;
#79559=EDGE_CURVE ( 'NONE', #136825, #10452, #65541, .T. ) ;
#79560=ORIENTED_EDGE ( 'NONE', *, *, #16847, .T. ) ;
#79562=DIRECTION ( 'NONE',  ( 0.7071067811865487940, 0.7071067811865463515, 0.000000000000000000 ) ) ;
#79565=CARTESIAN_POINT ( 'NONE',  ( 34.92499999999998295, -2.240707523384260824, 4.255531930566177401 ) ) ;
#79566=CARTESIAN_POINT ( 'NONE',  ( -0.005480084712502889671, 28.92564299267938210, 4.000000000000000000 ) ) ;
#79567=ADVANCED_FACE ( 'NONE', ( #30001 ), #118435, .F. ) ;
#79568=DIRECTION ( 'NONE',  ( -0.3543493200069162685, -0.000000000000000000, -0.9351131265310288487 ) ) ;
#79569=EDGE_CURVE ( 'NONE', #14243, #128877, #52466, .T. ) ;
#79570=AXIS2_PLACEMENT_3D ( 'NONE', #15938, #127616, #94253 ) ;
#79571=CARTESIAN_POINT ( 'NONE',  ( -35.00492477221173715, -5.240707523384228850, 12.38332538355504298 ) ) ;
#79572=CARTESIAN_POINT ( 'NONE',  ( 34.42499999999998295, 16.54139925780187781, 5.000000000000000000 ) ) ;
#79573=CARTESIAN_POINT ( 'NONE',  ( 39.48921356237310221, -27.52281430457082934, 5.000000000000000000 ) ) ;
#79575=LINE ( 'NONE', #44801, #113586 ) ;
#79576=VECTOR ( 'NONE', #120373, 1000.000000000000000 ) ;
#79577=EDGE_LOOP ( 'NONE', ( #18991, #76010, #60251, #34676 ) ) ;
#79580=DIRECTION ( 'NONE',  ( 0.6830127018922181881, 0.6830127018922202975, -0.2588190451025214056 ) ) ;
#79581=CARTESIAN_POINT ( 'NONE',  ( 18.71757738642554258, -21.73023691814492864, 5.000000000000000888 ) ) ;
#79584=EDGE_CURVE ( 'NONE', #17037, #84184, #86554, .T. ) ;
#79585=CARTESIAN_POINT ( 'NONE',  ( -15.00548008471250228, 28.92564299267927552, 4.000000000000000000 ) ) ;
#79586=CARTESIAN_POINT ( 'NONE',  ( -34.92500000000001137, -0.1833456135895722428, 4.500000000000000888 ) ) ;
#79587=ORIENTED_EDGE ( 'NONE', *, *, #133286, .T. ) ;
#79590=DIRECTION ( 'NONE',  ( 0.7071067811865487940, 0.7071067811865463515, 0.000000000000000000 ) ) ;
#79591=VERTEX_POINT ( 'NONE', #137732 ) ;
#79592=VECTOR ( 'NONE', #39350, 999.9999999999998863 ) ;
#79593=LINE ( 'NONE', #90408, #112452 ) ;
#79594=EDGE_CURVE ( 'NONE', #139774, #102386, #22665, .T. ) ;
#79597=VECTOR ( 'NONE', #76150, 1000.000000000000227 ) ;
#79598=CARTESIAN_POINT ( 'NONE',  ( -5.999999999999950262, -16.44781430457066662, 5.000000000000000000 ) ) ;
#79601=LINE ( 'NONE', #34612, #70481 ) ;
#79602=DIRECTION ( 'NONE',  ( 0.7071067811865486830, -0.7071067811865464625, -0.000000000000000000 ) ) ;
#79604=DIRECTION ( 'NONE',  ( 0.7071067811865486830, -0.7071067811865464625, -0.000000000000000000 ) ) ;
#79605=ADVANCED_FACE ( 'NONE', ( #115199 ), #15882, .F. ) ;
#79606=CARTESIAN_POINT ( 'NONE',  ( 59.99451991528749772, 28.92564299267980132, 4.000000000000000000 ) ) ;
#79607=ORIENTED_EDGE ( 'NONE', *, *, #116128, .T. ) ;
#79608=VECTOR ( 'NONE', #97468, 1000.000000000000000 ) ;
#79609=CARTESIAN_POINT ( 'NONE',  ( -23.99999999999983302, 10.93112307739207267, 4.000000000000000000 ) ) ;
#79610=ORIENTED_EDGE ( 'NONE', *, *, #80691, .F. ) ;
#79611=VECTOR ( 'NONE', #99612, 999.9999999999998863 ) ;
#79614=DIRECTION ( 'NONE',  ( 0.000000000000000000, -0.3543493200069153248, -0.9351131265310291818 ) ) ;
#79615=EDGE_CURVE ( 'NONE', #134155, #35701, #40727, .T. ) ;
#79616=CARTESIAN_POINT ( 'NONE',  ( 0.000000000000000000, 0.000000000000000000, 5.000000000000000000 ) ) ;
#79617=CARTESIAN_POINT ( 'NONE',  ( -63.18398860626900415, 28.73617430169831621, 5.000000000000000000 ) ) ;
#79618=ORIENTED_EDGE ( 'NONE', *, *, #86685, .T. ) ;
#79619=CARTESIAN_POINT ( 'NONE',  ( 26.99451991528749417, 28.92564299267956685, 4.000000000000000000 ) ) ;
#79622=CARTESIAN_POINT ( 'NONE',  ( 27.18398860626900060, 28.73617430169806042, 5.000000000000000000 ) ) ;
#79623=ORIENTED_EDGE ( 'NONE', *, *, #133756, .F. ) ;
#79624=CARTESIAN_POINT ( 'NONE',  ( -17.51078643762690845, -27.52281430457043143, 5.000000000000000000 ) ) ;
#79625=FACE_OUTER_BOUND ( 'NONE', #76977, .T. ) ;
#79627=EDGE_CURVE ( 'NONE', #52228, #24833, #60171, .T. ) ;
#79628=ORIENTED_EDGE ( 'NONE', *, *, #126456, .F. ) ;
#79629=FACE_OUTER_BOUND ( 'NONE', #140513, .T. ) ;
#79630=ADVANCED_FACE ( 'NONE', ( #99528 ), #81948, .T. ) ;
#79632=CARTESIAN_POINT ( 'NONE',  ( 9.241694584251812117, 0.7592924766157069794, 14.37146558664980489 ) ) ;
#79633=CARTESIAN_POINT ( 'NONE',  ( -2.816011393730999401, 28.73617430169785436, 5.000000000000000000 ) ) ;
#79634=LINE ( 'NONE', #112911, #65528 ) ;
#79635=VECTOR ( 'NONE', #107609, 1000.000000000000114 ) ;
#79638=ORIENTED_EDGE ( 'NONE', *, *, #17605, .F. ) ;
#79641=VECTOR ( 'NONE', #134786, 1000.000000000000000 ) ;
#79642=EDGE_LOOP ( 'NONE', ( #50815, #133844, #39919, #81176 ) ) ;
#79643=CARTESIAN_POINT ( 'NONE',  ( 29.50183651486025482, -17.24070752338410628, 8.407044977365156768 ) ) ;
#79644=CARTESIAN_POINT ( 'NONE',  ( -34.49999999999975842, 10.46425560840038038, 4.994342998332163219 ) ) ;
#79645=VECTOR ( 'NONE', #128942, 1000.000000000000000 ) ;
#79646=DIRECTION ( 'NONE',  ( 0.7071067811865487940, 0.7071067811865463515, 0.000000000000000000 ) ) ;
#79647=FACE_OUTER_BOUND ( 'NONE', #99193, .T. ) ;
#79648=ORIENTED_EDGE ( 'NONE', *, *, #141859, .T. ) ;
#79650=LINE ( 'NONE', #91213, #92985 ) ;
#79651=DIRECTION ( 'NONE',  ( -0.000000000000000000, 0.3543493200069153248, 0.9351131265310292928 ) ) ;
#79654=DIRECTION ( 'NONE',  ( -0.6830127018922181881, 0.6830127018922202975, -0.2588190451025214056 ) ) ;
#79655=VECTOR ( 'NONE', #59730, 1000.000000000000227 ) ;
#79656=DIRECTION ( 'NONE',  ( -0.000000000000000000, 0.3543493200069153248, 0.9351131265310292928 ) ) ;
#79657=ORIENTED_EDGE ( 'NONE', *, *, #8865, .F. ) ;
#79658=ORIENTED_EDGE ( 'NONE', *, *, #73675, .T. ) ;
#79659=FACE_OUTER_BOUND ( 'NONE', #54823, .T. ) ;
#79660=CARTESIAN_POINT ( 'NONE',  ( 8.671830600776420539, 14.25929247661558286, 4.000000000000000000 ) ) ;
#79661=VECTOR ( 'NONE', #109714, 999.9999999999998863 ) ;
#79662=CARTESIAN_POINT ( 'NONE',  ( 63.29974487139158867, -27.71228299555250274, 4.000000000000000000 ) ) ;
#79664=DIRECTION ( 'NONE',  ( -0.000000000000000000, -0.3543493200069152693, 0.9351131265310292928 ) ) ;
#79665=CARTESIAN_POINT ( 'NONE',  ( 54.18398860626899705, 28.73617430169825226, 5.000000000000000000 ) ) ;
#79666=VECTOR ( 'NONE', #143480, 1000.000000000000000 ) ;
#79668=VERTEX_POINT ( 'NONE', #197 ) ;
#79669=CARTESIAN_POINT ( 'NONE',  ( -27.18398860626900060, 28.73617430169806042, 5.000000000000000000 ) ) ;
#79670=ORIENTED_EDGE ( 'NONE', *, *, #130389, .T. ) ;
#79671=ADVANCED_FACE ( 'NONE', ( #114519 ), #134339, .F. ) ;
#79672=ORIENTED_EDGE ( 'NONE', *, *, #85559, .F. ) ;
#79673=VECTOR ( 'NONE', #10594, 1000.000000000000000 ) ;
#79674=DIRECTION ( 'NONE',  ( 0.7071067811865487940, 0.7071067811865463515, 0.000000000000000000 ) ) ;
#79675=ORIENTED_EDGE ( 'NONE', *, *, #134544, .F. ) ;
#79679=DIRECTION ( 'NONE',  ( -0.7071067811865486830, -0.7071067811865464625, 0.000000000000000000 ) ) ;
#79681=DIRECTION ( 'NONE',  ( 0.6830127018922180770, -0.6830127018922204085, -0.2588190451025213501 ) ) ;
#79682=ORIENTED_EDGE ( 'NONE', *, *, #108769, .T. ) ;
#79685=ORIENTED_EDGE ( 'NONE', *, *, #3640, .T. ) ;
#79686=LINE ( 'NONE', #143445, #16815 ) ;
#79688=CARTESIAN_POINT ( 'NONE',  ( 29.99999999999979039, -1.068876922607804314, 4.000000000000000000 ) ) ;
#79691=VERTEX_POINT ( 'NONE', #56810 ) ;
#79692=VECTOR ( 'NONE', #114897, 999.9999999999998863 ) ;
#79693=EDGE_LOOP ( 'NONE', ( #103590, #61593, #40681, #20300 ) ) ;
#79695=VECTOR ( 'NONE', #138582, 999.9999999999998863 ) ;
#79696=CARTESIAN_POINT ( 'NONE',  ( 0.7071067811865432429, -9.740707523384182664, 5.000000000000000000 ) ) ;
#79697=PLANE ( 'NONE',  #3184 ) ;
#79699=PLANE ( 'NONE',  #142345 ) ;
#79700=ADVANCED_FACE ( 'NONE', ( #45911 ), #90095, .F. ) ;
#79701=CARTESIAN_POINT ( 'NONE',  ( -66.48921356237309510, -27.52281430457101763, 5.000000000000000000 ) ) ;
#79702=CARTESIAN_POINT ( 'NONE',  ( -25.77325839282151065, -11.24070752338416845, 18.24660765846976673 ) ) ;
#79703=VECTOR ( 'NONE', #56883, 999.9999999999998863 ) ;
#79704=DIRECTION ( 'NONE',  ( -0.6830127018922181881, 0.6830127018922202975, -0.2588190451025214056 ) ) ;
#79705=EDGE_CURVE ( 'NONE', #5082, #9910, #94188, .T. ) ;
#79706=ORIENTED_EDGE ( 'NONE', *, *, #70247, .T. ) ;
#79707=DIRECTION ( 'NONE',  ( -0.7071067811865486830, -0.7071067811865464625, -0.000000000000000000 ) ) ;
#79708=AXIS2_PLACEMENT_3D ( 'NONE', #18863, #54397, #98571 ) ;
#79709=CARTESIAN_POINT ( 'NONE',  ( -6.005480084712508493, 28.92564299267933947, 4.000000000000000000 ) ) ;
#79710=AXIS2_PLACEMENT_3D ( 'NONE', #33603, #77803, #22654 ) ;
#79712=ORIENTED_EDGE ( 'NONE', *, *, #46836, .F. ) ;
#79713=LINE ( 'NONE', #68808, #21721 ) ;
#79714=EDGE_CURVE ( 'NONE', #117294, #105391, #39859, .T. ) ;
#79717=CARTESIAN_POINT ( 'NONE',  ( -31.49999999999977973, -5.568876922607755908, 4.000000000000000000 ) ) ;
#79718=PLANE ( 'NONE',  #1526 ) ;
#79719=VECTOR ( 'NONE', #32800, 999.9999999999998863 ) ;
#79720=DIRECTION ( 'NONE',  ( 1.000000000000000000, 0.000000000000000000, 0.000000000000000000 ) ) ;
#79721=LINE ( 'NONE', #47099, #134394 ) ;
#79723=ORIENTED_EDGE ( 'NONE', *, *, #117727, .F. ) ;
#79724=LINE ( 'NONE', #47103, #70040 ) ;
#79725=VECTOR ( 'NONE', #43446, 1000.000000000000000 ) ;
#79726=VECTOR ( 'NONE', #139040, 999.9999999999998863 ) ;
#79728=ORIENTED_EDGE ( 'NONE', *, *, #84535, .T. ) ;
#79731=FACE_OUTER_BOUND ( 'NONE', #36670, .T. ) ;
#79732=EDGE_LOOP ( 'NONE', ( #120039, #39458, #137164, #105310 ) ) ;
#79733=EDGE_CURVE ( 'NONE', #126893, #22921, #116666, .T. ) ;
#79734=VERTEX_POINT ( 'NONE', #7886 ) ;
#79735=VERTEX_POINT ( 'NONE', #27499 ) ;
#79737=CARTESIAN_POINT ( 'NONE',  ( -23.99999999999982592, -16.02097659208072855, -11.96015758381202865 ) ) ;
#79738=LINE ( 'NONE', #137646, #63573 ) ;
#79739=DIRECTION ( 'NONE',  ( -0.7071067811865487940, 0.7071067811865463515, 0.000000000000000000 ) ) ;
#79740=EDGE_LOOP ( 'NONE', ( #44675, #44492, #51496, #120473 ) ) ;
#79743=CARTESIAN_POINT ( 'NONE',  ( -27.32816939922334143, -15.74070752338412049, 4.000000000000000000 ) ) ;
#79744=CARTESIAN_POINT ( 'NONE',  ( 9.183988606268997046, 28.73617430169793607, 5.000000000000000000 ) ) ;
#79745=CARTESIAN_POINT ( 'NONE',  ( -42.29974487139158157, -27.71228299555235708, 4.000000000000000000 ) ) ;
#79746=EDGE_LOOP ( 'NONE', ( #4937, #139823, #67819, #95331 ) ) ;
#79748=FACE_OUTER_BOUND ( 'NONE', #49029, .T. ) ;
#79749=EDGE_CURVE ( 'NONE', #121955, #126191, #73193, .T. ) ;
#79750=ORIENTED_EDGE ( 'NONE', *, *, #123501, .T. ) ;
#79753=EDGE_CURVE ( 'NONE', #92724, #13174, #126815, .T. ) ;
#79755=EDGE_CURVE ( 'NONE', #50562, #91076, #6420, .T. ) ;
#79757=CARTESIAN_POINT ( 'NONE',  ( -54.18398860626899705, 28.73617430169825226, 5.000000000000000000 ) ) ;
#79758=ORIENTED_EDGE ( 'NONE', *, *, #141396, .F. ) ;
#79759=CARTESIAN_POINT ( 'NONE',  ( -34.75611968250420603, 8.812934254707275983, 4.955485411084900704 ) ) ;
#79760=ORIENTED_EDGE ( 'NONE', *, *, #33044, .T. ) ;
#79761=LINE ( 'NONE', #57993, #116996 ) ;
#79762=DIRECTION ( 'NONE',  ( 0.7071067811865487940, 0.7071067811865463515, 0.000000000000000000 ) ) ;
#79763=CARTESIAN_POINT ( 'NONE',  ( -80.99451991528748351, 28.92564299267994699, 4.000000000000000000 ) ) ;
#79764=EDGE_CURVE ( 'NONE', #135826, #135984, #28243, .T. ) ;
#79765=CARTESIAN_POINT ( 'NONE',  ( 23.81601139373100295, 28.73617430169770870, 5.000000000000000000 ) ) ;
#79766=PLANE ( 'NONE',  #111429 ) ;
#79767=PLANE ( 'NONE',  #25984 ) ;
#79768=CARTESIAN_POINT ( 'NONE',  ( 29.99999999999979394, -1.447814304570815169, 5.000000000000000000 ) ) ;
#79770=DIRECTION ( 'NONE',  ( -0.7071067811865486830, -0.7071067811865464625, 0.000000000000000000 ) ) ;
#79771=DIRECTION ( 'NONE',  ( -0.3543493200069162685, -0.000000000000000000, -0.9351131265310288487 ) ) ;
#79773=CARTESIAN_POINT ( 'NONE',  ( -7.446650576632133145, 2.259292476615690770, 14.86850063742356198 ) ) ;
#79774=DIRECTION ( 'NONE',  ( -0.6830127018922181881, 0.6830127018922202975, -0.2588190451025214056 ) ) ;
#79776=VECTOR ( 'NONE', #51994, 1000.000000000000000 ) ;
#79777=VERTEX_POINT ( 'NONE', #96306 ) ;
#79779=ORIENTED_EDGE ( 'NONE', *, *, #131492, .T. ) ;
#79780=VERTEX_POINT ( 'NONE', #139879 ) ;
#79781=VERTEX_POINT ( 'NONE', #129674 ) ;
#79782=CARTESIAN_POINT ( 'NONE',  ( 34.49999999999975131, -5.945670655168991736, 4.994342998332164996 ) ) ;
#79783=FACE_OUTER_BOUND ( 'NONE', #140938, .T. ) ;
#79784=FACE_OUTER_BOUND ( 'NONE', #58801, .T. ) ;
#79785=ORIENTED_EDGE ( 'NONE', *, *, #111046, .T. ) ;
#79786=CARTESIAN_POINT ( 'NONE',  ( 15.29974487139158867, -27.71228299555216879, 4.000000000000000000 ) ) ;
#79787=FACE_OUTER_BOUND ( 'NONE', #54413, .T. ) ;
#79788=CARTESIAN_POINT ( 'NONE',  ( 27.48921356237309155, -27.52281430457074762, 5.000000000000000000 ) ) ;
#79791=DIRECTION ( 'NONE',  ( 0.7071067811865486830, -0.7071067811865464625, -0.000000000000000000 ) ) ;
#79792=DIRECTION ( 'NONE',  ( -0.7071067811865487940, 0.7071067811865463515, -0.000000000000000000 ) ) ;
#79793=CARTESIAN_POINT ( 'NONE',  ( -17.70025512860841488, -27.71228299555193786, 4.000000000000000000 ) ) ;
#79795=VECTOR ( 'NONE', #56697, 999.9999999999998863 ) ;
#79796=DIRECTION ( 'NONE',  ( -0.7071067811865486830, -0.7071067811865464625, -0.000000000000000000 ) ) ;
#79797=LINE ( 'NONE', #91360, #5271 ) ;
#79798=DIRECTION ( 'NONE',  ( -0.7071067811865486830, 0.7071067811865464625, 0.000000000000000000 ) ) ;
#79799=CARTESIAN_POINT ( 'NONE',  ( 24.18398860626899705, 28.73617430169804265, 5.000000000000000000 ) ) ;
#79801=EDGE_CURVE ( 'NONE', #54679, #69767, #16630, .T. ) ;
#79802=EDGE_CURVE ( 'NONE', #46380, #27078, #117356, .T. ) ;
#79804=EDGE_LOOP ( 'NONE', ( #61310, #39286, #117872, #54659 ) ) ;
#79805=ORIENTED_EDGE ( 'NONE', *, *, #140825, .F. ) ;
#79807=EDGE_LOOP ( 'NONE', ( #23620, #116053, #42926, #76221, #124303, #19911 ) ) ;
#79808=VECTOR ( 'NONE', #124839, 1000.000000000000000 ) ;
#79811=DIRECTION ( 'NONE',  ( -0.7071067811865487940, 0.7071067811865463515, -0.000000000000000000 ) ) ;
#79812=PLANE ( 'NONE',  #120697 ) ;
#79814=VECTOR ( 'NONE', #131761, 1000.000000000000000 ) ;
#79815=ORIENTED_EDGE ( 'NONE', *, *, #84644, .T. ) ;
#79816=ORIENTED_EDGE ( 'NONE', *, *, #3479, .F. ) ;
#79817=CARTESIAN_POINT ( 'NONE',  ( -5.292893218813416567, 2.259292476615692546, 5.000000000000000000 ) ) ;
#79818=FACE_OUTER_BOUND ( 'NONE', #44613, .T. ) ;
#79819=ORIENTED_EDGE ( 'NONE', *, *, #53124, .T. ) ;
#79821=ORIENTED_EDGE ( 'NONE', *, *, #92658, .F. ) ;
#79822=CARTESIAN_POINT ( 'NONE',  ( -16.49999999999988276, -11.56887692260769285, 4.000000000000000000 ) ) ;
#79824=VECTOR ( 'NONE', #72380, 1000.000000000000114 ) ;
#79826=VECTOR ( 'NONE', #130517, 1000.000000000000227 ) ;
#79828=ORIENTED_EDGE ( 'NONE', *, *, #130123, .F. ) ;
#79829=VECTOR ( 'NONE', #131864, 999.9999999999998863 ) ;
#79831=DIRECTION ( 'NONE',  ( -0.000000000000000000, -0.3543493200069152693, 0.9351131265310292928 ) ) ;
#79832=ORIENTED_EDGE ( 'NONE', *, *, #70739, .F. ) ;
#79833=VERTEX_POINT ( 'NONE', #83339 ) ;
#79834=VERTEX_POINT ( 'NONE', #72504 ) ;
#79835=CARTESIAN_POINT ( 'NONE',  ( 25.49999999999982592, -7.533600742197662292, 5.000000000000000000 ) ) ;
#79836=VECTOR ( 'NONE', #103318, 1000.000000000000000 ) ;
#79837=DIRECTION ( 'NONE',  ( -0.7071067811865486830, 0.7071067811865464625, 0.000000000000000000 ) ) ;
#79838=CARTESIAN_POINT ( 'NONE',  ( -34.92500000000001137, -21.18334561358935986, 4.500000000000000888 ) ) ;
#79839=ORIENTED_EDGE ( 'NONE', *, *, #127275, .T. ) ;
#79840=CARTESIAN_POINT ( 'NONE',  ( -34.42500000000001137, 19.54139925780181386, 5.000000000000000000 ) ) ;
#79841=CARTESIAN_POINT ( 'NONE',  ( 69.18398860626899705, 28.73617430169835529, 5.000000000000000000 ) ) ;
#79842=FACE_OUTER_BOUND ( 'NONE', #14310, .T. ) ;
#79843=EDGE_CURVE ( 'NONE', #133751, #11858, #74980, .T. ) ;
#79844=FACE_BOUND ( 'NONE', #3285, .T. ) ;
#79845=EDGE_LOOP ( 'NONE', ( #76986, #87031, #65752, #100082 ) ) ;
#79846=CARTESIAN_POINT ( 'NONE',  ( 42.48921356237308800, -27.52281430457085065, 5.000000000000000000 ) ) ;
#79847=EDGE_CURVE ( 'NONE', #125405, #87449, #105763, .T. ) ;
#79849=ADVANCED_FACE ( 'NONE', ( #139160 ), #84080, .F. ) ;
#79850=CARTESIAN_POINT ( 'NONE',  ( -27.70710678118634718, 5.259292476615662792, 5.000000000000000000 ) ) ;
#79851=VERTEX_POINT ( 'NONE', #107213 ) ;
#79852=FACE_OUTER_BOUND ( 'NONE', #134699, .T. ) ;
#79853=ORIENTED_EDGE ( 'NONE', *, *, #50869, .T. ) ;
#79854=VERTEX_POINT ( 'NONE', #89063 ) ;
#79859=VERTEX_POINT ( 'NONE', #86909 ) ;
#79860=DIRECTION ( 'NONE',  ( -0.7071067811865486830, -0.7071067811865464625, -0.000000000000000000 ) ) ;
#79861=CARTESIAN_POINT ( 'NONE',  ( -27.18398860626900060, 28.73617430169806042, 5.000000000000000000 ) ) ;
#79862=EDGE_CURVE ( 'NONE', #92065, #100356, #120260, .T. ) ;
#79863=ORIENTED_EDGE ( 'NONE', *, *, #142080, .T. ) ;
#79864=DIRECTION ( 'NONE',  ( -0.3543493200069162685, -0.000000000000000000, -0.9351131265310288487 ) ) ;
#79865=LINE ( 'NONE', #45093, #85159 ) ;
#79866=AXIS2_PLACEMENT_3D ( 'NONE', #89793, #36152, #58666 ) ;
#79867=EDGE_CURVE ( 'NONE', #76506, #135631, #131839, .T. ) ;
#79869=CARTESIAN_POINT ( 'NONE',  ( 36.18398860626899705, 28.73617430169812437, 5.000000000000000000 ) ) ;
#79871=ORIENTED_EDGE ( 'NONE', *, *, #76703, .F. ) ;
#79872=EDGE_LOOP ( 'NONE', ( #5149, #71433, #96451, #128678 ) ) ;
#79873=ORIENTED_EDGE ( 'NONE', *, *, #133989, .T. ) ;
#79874=ORIENTED_EDGE ( 'NONE', *, *, #99024, .T. ) ;
#79875=PLANE ( 'NONE',  #7691 ) ;
#79877=EDGE_LOOP ( 'NONE', ( #57097, #54986, #69103, #58678 ) ) ;
#79878=ORIENTED_EDGE ( 'NONE', *, *, #42467, .T. ) ;
#79880=DIRECTION ( 'NONE',  ( -0.6830127018922180770, -0.6830127018922204085, -0.2588190451025213501 ) ) ;
#79881=DIRECTION ( 'NONE',  ( 0.7071067811865487940, 0.7071067811865463515, -0.000000000000000000 ) ) ;
#79883=DIRECTION ( 'NONE',  ( -0.7071067811865486830, -0.7071067811865464625, 0.000000000000000000 ) ) ;
#79886=( BOUNDED_CURVE ( )  B_SPLINE_CURVE ( 3, ( #73602, #14914, #115623, #62029 ),
 .UNSPECIFIED., .F., .T. ) 
 B_SPLINE_CURVE_WITH_KNOTS ( ( 4, 4 ),
 ( 5.920967161967926273, 7.341195215986592970 ),
 .UNSPECIFIED. ) 
 CURVE ( )  GEOMETRIC_REPRESENTATION_ITEM ( )  RATIONAL_B_SPLINE_CURVE ( ( 1.000000000000000000, 0.8388583629366708205, 0.8388583629366708205, 1.000000000000000000 ) ) 
 REPRESENTATION_ITEM ( '' )  );
#79887=DIRECTION ( 'NONE',  ( -0.6830127018922181881, 0.6830127018922202975, -0.2588190451025214056 ) ) ;
#79888=VECTOR ( 'NONE', #101315, 999.9999999999998863 ) ;
#79890=DIRECTION ( 'NONE',  ( -0.000000000000000000, 0.000000000000000000, 1.000000000000000000 ) ) ;
#79894=CARTESIAN_POINT ( 'NONE',  ( -21.48921356237309155, -27.52281430457070499, 5.000000000000000000 ) ) ;
#79895=CARTESIAN_POINT ( 'NONE',  ( -23.99451991528749062, 28.92564299267954908, 4.000000000000000000 ) ) ;
#79896=EDGE_CURVE ( 'NONE', #28591, #108745, #32528, .T. ) ;
#79897=ORIENTED_EDGE ( 'NONE', *, *, #109620, .F. ) ;
#79898=CARTESIAN_POINT ( 'NONE',  ( 27.48921356237309155, -27.52281430457074762, 5.000000000000000000 ) ) ;
#79899=LINE ( 'NONE', #24747, #112058 ) ;
#79900=ORIENTED_EDGE ( 'NONE', *, *, #101502, .F. ) ;
#79901=CARTESIAN_POINT ( 'NONE',  ( -22.49999999999984013, -10.04351517176480257, -1.623559851933875198 ) ) ;
#79902=VERTEX_POINT ( 'NONE', #142709 ) ;
#79903=DIRECTION ( 'NONE',  ( -0.000000000000000000, -0.3543493200069152693, 0.9351131265310292928 ) ) ;
#79905=PLANE ( 'NONE',  #100220 ) ;
#79906=CARTESIAN_POINT ( 'NONE',  ( -29.99999999999979039, -21.84840872380826937, 2.849755605029536731 ) ) ;
#79907=EDGE_LOOP ( 'NONE', ( #4373, #75774, #105996, #97865 ) ) ;
#79908=EDGE_CURVE ( 'NONE', #110472, #61139, #64427, .T. ) ;
#79909=VECTOR ( 'NONE', #14948, 1000.000000000000000 ) ;
#79910=EDGE_CURVE ( 'NONE', #96370, #88116, #133283, .T. ) ;
#79911=PLANE ( 'NONE',  #11714 ) ;
#79912=CARTESIAN_POINT ( 'NONE',  ( -5.999999999999963585, -10.06887692260771061, 4.000000000000000000 ) ) ;
#79913=ORIENTED_EDGE ( 'NONE', *, *, #76948, .F. ) ;
#79914=LINE ( 'NONE', #4368, #30793 ) ;
#79915=ADVANCED_FACE ( 'NONE', ( #132584 ), #582, .F. ) ;
#79916=ORIENTED_EDGE ( 'NONE', *, *, #4547, .T. ) ;
#79917=CARTESIAN_POINT ( 'NONE',  ( -3.098435806082346922, 11.25929247661560240, 10.79108189686406405 ) ) ;
#79918=FACE_OUTER_BOUND ( 'NONE', #109421, .T. ) ;
#79919=ORIENTED_EDGE ( 'NONE', *, *, #101061, .F. ) ;
#79920=ORIENTED_EDGE ( 'NONE', *, *, #14651, .F. ) ;
#79922=VERTEX_POINT ( 'NONE', #120944 ) ;
#79924=VECTOR ( 'NONE', #61855, 1000.000000000000000 ) ;
#79926=VECTOR ( 'NONE', #71645, 1000.000000000000000 ) ;
#79928=DIRECTION ( 'NONE',  ( -0.6830127018922180770, -0.6830127018922204085, -0.2588190451025213501 ) ) ;
#79929=DIRECTION ( 'NONE',  ( 0.7071067811865487940, 0.7071067811865463515, 0.000000000000000000 ) ) ;
#79931=DIRECTION ( 'NONE',  ( -0.7071067811865486830, -0.7071067811865464625, 0.000000000000000000 ) ) ;
#79932=CARTESIAN_POINT ( 'NONE',  ( 20.99999999999985789, -9.412538124160656494, 4.000000000000000000 ) ) ;
#79935=ORIENTED_EDGE ( 'NONE', *, *, #67268, .T. ) ;
#79936=ORIENTED_EDGE ( 'NONE', *, *, #23752, .F. ) ;
#79941=VERTEX_POINT ( 'NONE', #66588 ) ;
#79943=LINE ( 'NONE', #34256, #16186 ) ;
#79944=ORIENTED_EDGE ( 'NONE', *, *, #28176, .T. ) ;
#79945=LINE ( 'NONE', #56767, #41582 ) ;
#79947=DIRECTION ( 'NONE',  ( 0.7071067811865486830, -0.7071067811865464625, -0.000000000000000000 ) ) ;
#79948=CARTESIAN_POINT ( 'NONE',  ( -23.51078643762690490, -27.52281430457038880, 5.000000000000000000 ) ) ;
#79950=ORIENTED_EDGE ( 'NONE', *, *, #55378, .T. ) ;
#79951=EDGE_CURVE ( 'NONE', #129972, #132519, #22316, .T. ) ;
#79952=LINE ( 'NONE', #2305, #111205 ) ;
#79953=CARTESIAN_POINT ( 'NONE',  ( -30.78162688292473348, 21.74787736706806385, 4.999607392498049308 ) ) ;
#79954=DIRECTION ( 'NONE',  ( -0.3543493200069162685, -0.000000000000000000, -0.9351131265310288487 ) ) ;
#79955=CARTESIAN_POINT ( 'NONE',  ( -26.99451991528749417, 28.92564299267956685, 4.000000000000000000 ) ) ;
#79956=FACE_OUTER_BOUND ( 'NONE', #30087, .T. ) ;
#79957=CARTESIAN_POINT ( 'NONE',  ( 17.47599861414538580, 22.03583458319439359, 4.979811245910084949 ) ) ;
#79958=PLANE ( 'NONE',  #64326 ) ;
#79960=CARTESIAN_POINT ( 'NONE',  ( -34.92500000000001137, -22.22500000000000142, 4.500000000000000888 ) ) ;
#79962=FACE_OUTER_BOUND ( 'NONE', #123077, .T. ) ;
#79963=ORIENTED_EDGE ( 'NONE', *, *, #23127, .F. ) ;
#79964=ORIENTED_EDGE ( 'NONE', *, *, #59702, .T. ) ;
#79968=DIRECTION ( 'NONE',  ( -0.000000000000000000, 0.3543493200069153248, 0.9351131265310292928 ) ) ;
#79969=ORIENTED_EDGE ( 'NONE', *, *, #135005, .T. ) ;
#79970=DIRECTION ( 'NONE',  ( -0.7071067811865486830, 0.7071067811865464625, 0.000000000000000000 ) ) ;
#79972=FACE_OUTER_BOUND ( 'NONE', #121389, .T. ) ;
#79973=EDGE_CURVE ( 'NONE', #72893, #129741, #91887, .T. ) ;
#79975=ORIENTED_EDGE ( 'NONE', *, *, #84442, .F. ) ;
#79976=CARTESIAN_POINT ( 'NONE',  ( -21.48921356237309155, -27.52281430457070499, 5.000000000000000000 ) ) ;
#79977=EDGE_LOOP ( 'NONE', ( #133250, #87913, #4399, #14570 ) ) ;
#79978=DIRECTION ( 'NONE',  ( -0.000000000000000000, -0.3543493200069152693, 0.9351131265310292928 ) ) ;
#79980=DIRECTION ( 'NONE',  ( -0.6830127018922181881, 0.6830127018922202975, -0.2588190451025214056 ) ) ;
#79981=CARTESIAN_POINT ( 'NONE',  ( -30.18398860626900060, 28.73617430169808173, 5.000000000000000000 ) ) ;
#79982=ORIENTED_EDGE ( 'NONE', *, *, #83670, .T. ) ;
#79983=EDGE_CURVE ( 'NONE', #41151, #105272, #81039, .T. ) ;
#79985=VERTEX_POINT ( 'NONE', #12888 ) ;
#79986=DIRECTION ( 'NONE',  ( 1.000000000000000000, 0.000000000000000000, 0.000000000000000000 ) ) ;
#79987=LINE ( 'NONE', #44498, #78647 ) ;
#79988=PLANE ( 'NONE',  #75532 ) ;
#79989=DIRECTION ( 'NONE',  ( -0.7071067811865486830, -0.7071067811865464625, -0.000000000000000000 ) ) ;
#79990=FACE_OUTER_BOUND ( 'NONE', #51076, .T. ) ;
#79994=VECTOR ( 'NONE', #77996, 1000.000000000000000 ) ;
#79995=DIRECTION ( 'NONE',  ( 0.7071067811865487940, 0.7071067811865463515, 0.000000000000000000 ) ) ;
#79996=LINE ( 'NONE', #49510, #6140 ) ;
#79997=DIRECTION ( 'NONE',  ( 0.7071067811865487940, -0.7071067811865463515, 0.000000000000000000 ) ) ;
#79998=ORIENTED_EDGE ( 'NONE', *, *, #32114, .T. ) ;
#79999=EDGE_LOOP ( 'NONE', ( #67986, #7778, #137359, #36334 ) ) ;
#80000=CARTESIAN_POINT ( 'NONE',  ( 23.99999999999983302, 4.384688058510586295, -7.090945410444628116 ) ) ;
#80001=ORIENTED_EDGE ( 'NONE', *, *, #125759, .F. ) ;
#80002=ADVANCED_FACE ( 'NONE', ( #59995 ), #57167, .T. ) ;
#80003=AXIS2_PLACEMENT_3D ( 'NONE', #55112, #89852, #24602 ) ;
#80005=ORIENTED_EDGE ( 'NONE', *, *, #49553, .T. ) ;
#80006=DIRECTION ( 'NONE',  ( 0.000000000000000000, 1.000000000000000000, 0.000000000000000000 ) ) ;
#80007=EDGE_CURVE ( 'NONE', #21679, #92143, #68744, .T. ) ;
#80009=FACE_BOUND ( 'NONE', #135794, .T. ) ;
#80010=DIRECTION ( 'NONE',  ( 0.7071067811865486830, 0.7071067811865463515, 0.000000000000000000 ) ) ;
#80011=EDGE_CURVE ( 'NONE', #88361, #100840, #68060, .T. ) ;
#80012=EDGE_CURVE ( 'NONE', #141003, #26697, #78907, .T. ) ;
#80013=LINE ( 'NONE', #227, #95241 ) ;
#80014=LINE ( 'NONE', #10410, #59618 ) ;
#80015=LINE ( 'NONE', #113296, #94432 ) ;
#80016=ORIENTED_EDGE ( 'NONE', *, *, #35043, .F. ) ;
#80017=VERTEX_POINT ( 'NONE', #35416 ) ;
#80018=CARTESIAN_POINT ( 'NONE',  ( 0.000000000000000000, 0.000000000000000000, 5.000000000000000000 ) ) ;
#80019=VECTOR ( 'NONE', #51408, 1000.000000000000000 ) ;
#80020=ORIENTED_EDGE ( 'NONE', *, *, #86841, .F. ) ;
#80021=EDGE_CURVE ( 'NONE', #31148, #96439, #34671, .T. ) ;
#80022=EDGE_CURVE ( 'NONE', #82135, #8845, #124528, .T. ) ;
#80024=ORIENTED_EDGE ( 'NONE', *, *, #65344, .T. ) ;
#80026=VERTEX_POINT ( 'NONE', #25196 ) ;
#80027=EDGE_CURVE ( 'NONE', #106377, #4302, #102060, .T. ) ;
#80028=AXIS2_PLACEMENT_3D ( 'NONE', #137609, #128165, #28841 ) ;
#80029=PLANE ( 'NONE',  #69554 ) ;
#80030=EDGE_CURVE ( 'NONE', #94256, #10011, #36109, .T. ) ;
#80031=VERTEX_POINT ( 'NONE', #90474 ) ;
#80032=AXIS2_PLACEMENT_3D ( 'NONE', #29413, #136744, #37460 ) ;
#80033=EDGE_CURVE ( 'NONE', #108713, #88501, #15708, .T. ) ;
#80034=FACE_OUTER_BOUND ( 'NONE', #78846, .T. ) ;
#80035=EDGE_CURVE ( 'NONE', #112402, #33663, #24491, .T. ) ;
#80036=DIRECTION ( 'NONE',  ( -0.7071067811865486830, -0.7071067811865464625, 0.000000000000000000 ) ) ;
#80037=CARTESIAN_POINT ( 'NONE',  ( -18.18398860626898994, 28.73617430169800002, 5.000000000000000000 ) ) ;
#80038=DIRECTION ( 'NONE',  ( 0.6830127018922180770, -0.6830127018922204085, -0.2588190451025213501 ) ) ;
#80039=CARTESIAN_POINT ( 'NONE',  ( 18.79289321881332242, -17.24070752338410983, 5.000000000000000000 ) ) ;
#80041=ORIENTED_EDGE ( 'NONE', *, *, #1876, .F. ) ;
#80042=CARTESIAN_POINT ( 'NONE',  ( 24.99033360189226016, 3.759292476615681888, 4.478963035907999490 ) ) ;
#80043=CARTESIAN_POINT ( 'NONE',  ( 45.48921356237309510, -27.52281430457087197, 5.000000000000000000 ) ) ;
#80044=ORIENTED_EDGE ( 'NONE', *, *, #86927, .T. ) ;
#80045=EDGE_CURVE ( 'NONE', #137395, #83728, #25931, .T. ) ;
#80046=ORIENTED_EDGE ( 'NONE', *, *, #118769, .F. ) ;
#80047=EDGE_LOOP ( 'NONE', ( #59657, #119621, #15735, #20005 ) ) ;
#80050=ORIENTED_EDGE ( 'NONE', *, *, #62965, .F. ) ;
#80051=DIRECTION ( 'NONE',  ( -0.3543493200069162685, -0.000000000000000000, -0.9351131265310288487 ) ) ;
#80052=ADVANCED_FACE ( 'NONE', ( #80338 ), #69453, .F. ) ;
#80053=CARTESIAN_POINT ( 'NONE',  ( 45.18398860626900415, 28.73617430169818832, 5.000000000000000000 ) ) ;
#80055=CARTESIAN_POINT ( 'NONE',  ( -25.65788372223791569, 22.22500000000000142, 1.488343219358003067 ) ) ;
#80056=ORIENTED_EDGE ( 'NONE', *, *, #93425, .T. ) ;
#80057=DIRECTION ( 'NONE',  ( -0.3543493200069162685, -0.000000000000000000, -0.9351131265310288487 ) ) ;
#80059=LINE ( 'NONE', #122076, #133189 ) ;
#80060=LINE ( 'NONE', #101042, #132870 ) ;
#80061=ORIENTED_EDGE ( 'NONE', *, *, #42204, .T. ) ;
#80062=ORIENTED_EDGE ( 'NONE', *, *, #35265, .T. ) ;
#80063=FACE_OUTER_BOUND ( 'NONE', #16915, .T. ) ;
#80065=VERTEX_POINT ( 'NONE', #4102 ) ;
#80067=EDGE_CURVE ( 'NONE', #111354, #37298, #48386, .T. ) ;
#80068=CARTESIAN_POINT ( 'NONE',  ( -39.18398860626899705, 28.73617430169814568, 5.000000000000000000 ) ) ;
#80072=CARTESIAN_POINT ( 'NONE',  ( -26.99999999999980460, 20.58746187583902909, 4.000000000000000000 ) ) ;
#80073=ORIENTED_EDGE ( 'NONE', *, *, #103436, .T. ) ;
#80075=DIRECTION ( 'NONE',  ( 0.6830127018922181881, 0.6830127018922202975, -0.2588190451025214056 ) ) ;
#80076=EDGE_CURVE ( 'NONE', #23783, #127787, #18581, .T. ) ;
#80078=DIRECTION ( 'NONE',  ( -0.000000000000000000, 0.000000000000000000, 1.000000000000000000 ) ) ;
#80079=CARTESIAN_POINT ( 'NONE',  ( -9.707106781186475075, 11.25929247661560773, 5.000000000000000000 ) ) ;
#80080=VERTEX_POINT ( 'NONE', #71579 ) ;
#80082=LINE ( 'NONE', #45312, #118787 ) ;
#80083=VECTOR ( 'NONE', #108605, 1000.000000000000227 ) ;
#80084=CARTESIAN_POINT ( 'NONE',  ( -26.34505516254601076, 5.259292476615672562, 12.77922209995887393 ) ) ;
#80085=LINE ( 'NONE', #124265, #60096 ) ;
#80086=DIRECTION ( 'NONE',  ( -0.7071067811865486830, -0.7071067811865464625, 0.000000000000000000 ) ) ;
#80087=CARTESIAN_POINT ( 'NONE',  ( 26.99999999999980815, -13.97847968911258043, -0.1324546996126166887 ) ) ;
#80088=ORIENTED_EDGE ( 'NONE', *, *, #10443, .T. ) ;
#80089=EDGE_CURVE ( 'NONE', #127258, #4075, #61453, .T. ) ;
#80090=PLANE ( 'NONE',  #62726 ) ;
#80091=DIRECTION ( 'NONE',  ( 0.7071067811865486830, -0.7071067811865464625, -0.000000000000000000 ) ) ;
#80092=DIRECTION ( 'NONE',  ( 0.6830127018922181881, 0.6830127018922202975, -0.2588190451025214056 ) ) ;
#80094=( BOUNDED_CURVE ( )  B_SPLINE_CURVE ( 3, ( #5259, #85681, #127798, #62539 ),
 .UNSPECIFIED., .F., .F. ) 
 B_SPLINE_CURVE_WITH_KNOTS ( ( 4, 4 ),
 ( 1.864375635226932282, 1.933014472006549189 ),
 .UNSPECIFIED. ) 
 CURVE ( )  GEOMETRIC_REPRESENTATION_ITEM ( )  RATIONAL_B_SPLINE_CURVE ( ( 1.000000000000000000, 0.9996074310407763175, 0.9996074310407763175, 1.000000000000000000 ) ) 
 REPRESENTATION_ITEM ( '' )  );
#80095=DIRECTION ( 'NONE',  ( 0.6830127018922180770, -0.6830127018922204085, -0.2588190451025213501 ) ) ;
#80096=CARTESIAN_POINT ( 'NONE',  ( -34.49999999999976552, 6.054329344830883031, 4.994342998332166772 ) ) ;
#80097=CARTESIAN_POINT ( 'NONE',  ( -27.29974487139158512, -27.71228299555225405, 4.000000000000000000 ) ) ;
#80098=EDGE_CURVE ( 'NONE', #65481, #62418, #16553, .T. ) ;
#80099=ORIENTED_EDGE ( 'NONE', *, *, #109144, .F. ) ;
#80103=DIRECTION ( 'NONE',  ( -0.7071067811865487940, 0.7071067811865463515, 0.000000000000000000 ) ) ;
#80104=LINE ( 'NONE', #67065, #72123 ) ;
#80105=DIRECTION ( 'NONE',  ( 0.6830127018922181881, 0.6830127018922202975, -0.2588190451025214056 ) ) ;
#80106=EDGE_CURVE ( 'NONE', #42811, #98176, #104907, .T. ) ;
#80107=DIRECTION ( 'NONE',  ( -0.7071067811865486830, -0.7071067811865464625, -0.000000000000000000 ) ) ;
#80108=DIRECTION ( 'NONE',  ( 0.7071067811865487940, -0.7071067811865463515, 0.000000000000000000 ) ) ;
#80109=VERTEX_POINT ( 'NONE', #51261 ) ;
#80110=ORIENTED_EDGE ( 'NONE', *, *, #84467, .F. ) ;
#80111=LINE ( 'NONE', #112011, #115740 ) ;
#80113=CARTESIAN_POINT ( 'NONE',  ( -17.99999999999986855, -15.03360074219758680, 5.000000000000000000 ) ) ;
#80116=LINE ( 'NONE', #118214, #71805 ) ;
#80117=ADVANCED_FACE ( 'NONE', ( #138259 ), #19331, .F. ) ;
#80118=VECTOR ( 'NONE', #66219, 1000.000000000000000 ) ;
#80119=LINE ( 'NONE', #110542, #62302 ) ;
#80120=ORIENTED_EDGE ( 'NONE', *, *, #131407, .T. ) ;
#80123=DIRECTION ( 'NONE',  ( 0.7071067811865487940, -0.7071067811865463515, 0.000000000000000000 ) ) ;
#80124=AXIS2_PLACEMENT_3D ( 'NONE', #39279, #138585, #106627 ) ;
#80125=CARTESIAN_POINT ( 'NONE',  ( -36.48921356237310221, -27.52281430457080802, 5.000000000000000000 ) ) ;
#80126=LINE ( 'NONE', #2494, #8036 ) ;
#80129=EDGE_CURVE ( 'NONE', #60169, #94753, #28796, .T. ) ;
#80130=CARTESIAN_POINT ( 'NONE',  ( -12.98911971346042904, -22.02621442084247505, 4.990779571109221990 ) ) ;
#80131=EDGE_CURVE ( 'NONE', #58696, #120651, #94019, .T. ) ;
#80134=CARTESIAN_POINT ( 'NONE',  ( -15.49816348513947339, -17.24070752338410628, 8.407044977365259797 ) ) ;
#80136=ORIENTED_EDGE ( 'NONE', *, *, #119766, .T. ) ;
#80137=LINE ( 'NONE', #124318, #89396 ) ;
#80138=CARTESIAN_POINT ( 'NONE',  ( 21.18398860626899349, 28.73617430169802134, 5.000000000000000000 ) ) ;
#80139=CARTESIAN_POINT ( 'NONE',  ( -13.10362284818588741, 2.655808543615126638, 5.000000000000000000 ) ) ;
#80140=ADVANCED_FACE ( 'NONE', ( #105596 ), #118635, .F. ) ;
#80141=DIRECTION ( 'NONE',  ( -0.3543493200069162685, -0.000000000000000000, -0.9351131265310288487 ) ) ;
#80143=VERTEX_POINT ( 'NONE', #39682 ) ;
#80144=LINE ( 'NONE', #89553, #34563 ) ;
#80145=LINE ( 'NONE', #78687, #133292 ) ;
#80146=DIRECTION ( 'NONE',  ( 0.3543493200069162685, -0.000000000000000000, -0.9351131265310288487 ) ) ;
#80147=DIRECTION ( 'NONE',  ( 1.000000000000000000, 0.000000000000000000, 0.000000000000000000 ) ) ;
#80148=ORIENTED_EDGE ( 'NONE', *, *, #47432, .T. ) ;
#80149=ORIENTED_EDGE ( 'NONE', *, *, #138287, .F. ) ;
#80151=ORIENTED_EDGE ( 'NONE', *, *, #79307, .T. ) ;
#80152=CARTESIAN_POINT ( 'NONE',  ( -30.79289321881324071, 15.75929247661555443, 5.000000000000000000 ) ) ;
#80153=DIRECTION ( 'NONE',  ( 0.7071067811865486830, -0.7071067811865464625, -0.000000000000000000 ) ) ;
#80154=DIRECTION ( 'NONE',  ( 0.7071067811865487940, -0.7071067811865463515, 0.000000000000000000 ) ) ;
#80155=DIRECTION ( 'NONE',  ( 0.7071067811865487940, 0.7071067811865463515, -0.000000000000000000 ) ) ;
#80156=ORIENTED_EDGE ( 'NONE', *, *, #19301, .T. ) ;
#80157=ORIENTED_EDGE ( 'NONE', *, *, #105148, .T. ) ;
#80158=VECTOR ( 'NONE', #5538, 999.9999999999998863 ) ;
#80161=ORIENTED_EDGE ( 'NONE', *, *, #61691, .T. ) ;
#80162=DIRECTION ( 'NONE',  ( 0.000000000000000000, -0.3543493200069152138, 0.9351131265310292928 ) ) ;
#80163=ORIENTED_EDGE ( 'NONE', *, *, #99421, .T. ) ;
#80164=EDGE_CURVE ( 'NONE', #63701, #11751, #117187, .T. ) ;
#80165=LINE ( 'NONE', #121485, #59615 ) ;
#80167=EDGE_LOOP ( 'NONE', ( #62037, #9174, #97950, #2944 ) ) ;
#80168=FACE_BOUND ( 'NONE', #130407, .T. ) ;
#80169=CARTESIAN_POINT ( 'NONE',  ( 25.17183060077630330, 21.75929247661549937, 4.000000000000000000 ) ) ;
#80170=ADVANCED_FACE ( 'NONE', ( #83913 ), #16442, .T. ) ;
#80171=CARTESIAN_POINT ( 'NONE',  ( 0.000000000000000000, 0.000000000000000000, 5.000000000000000000 ) ) ;
#80172=CARTESIAN_POINT ( 'NONE',  ( 21.18398860626899349, 28.73617430169802134, 5.000000000000000000 ) ) ;
#80173=DIRECTION ( 'NONE',  ( -0.7071067811865487940, 0.7071067811865463515, 0.000000000000000000 ) ) ;
#80174=DIRECTION ( 'NONE',  ( 0.7071067811865487940, 0.7071067811865463515, -0.000000000000000000 ) ) ;
#80177=VERTEX_POINT ( 'NONE', #96150 ) ;
#80178=EDGE_CURVE ( 'NONE', #43125, #46125, #127369, .T. ) ;
#80179=VERTEX_POINT ( 'NONE', #104162 ) ;
#80181=ORIENTED_EDGE ( 'NONE', *, *, #96800, .F. ) ;
#80183=VECTOR ( 'NONE', #115750, 1000.000000000000227 ) ;
#80184=LINE ( 'NONE', #137400, #85969 ) ;
#80185=ORIENTED_EDGE ( 'NONE', *, *, #59143, .F. ) ;
#80187=DIRECTION ( 'NONE',  ( 0.7071067811865487940, 0.7071067811865463515, 0.000000000000000000 ) ) ;
#80188=EDGE_CURVE ( 'NONE', #6977, #35122, #93322, .T. ) ;
#80189=DIRECTION ( 'NONE',  ( -0.7071067811865486830, -0.7071067811865464625, -0.000000000000000000 ) ) ;
#80190=LINE ( 'NONE', #58469, #61112 ) ;
#80191=VERTEX_POINT ( 'NONE', #106295 ) ;
#80195=EDGE_CURVE ( 'NONE', #10002, #114801, #40395, .T. ) ;
#80197=CARTESIAN_POINT ( 'NONE',  ( -5.999999999999960032, 10.93112307739207623, 4.000000000000000000 ) ) ;
#80198=CARTESIAN_POINT ( 'NONE',  ( -8.004924772211888140, -5.240707523384228850, 12.38332538355497903 ) ) ;
#80199=ORIENTED_EDGE ( 'NONE', *, *, #45766, .F. ) ;
#80200=DIRECTION ( 'NONE',  ( -0.000000000000000000, 0.3543493200069153248, 0.9351131265310292928 ) ) ;
#80202=EDGE_CURVE ( 'NONE', #11599, #33380, #137556, .T. ) ;
#80204=VECTOR ( 'NONE', #56459, 1000.000000000000000 ) ;
#80205=ORIENTED_EDGE ( 'NONE', *, *, #99435, .T. ) ;
#80206=ADVANCED_FACE ( 'NONE', ( #99738 ), #141845, .F. ) ;
#80207=ORIENTED_EDGE ( 'NONE', *, *, #113326, .T. ) ;
#80209=EDGE_LOOP ( 'NONE', ( #132484, #77359, #39643, #23804 ) ) ;
#80210=ADVANCED_FACE ( 'NONE', ( #407 ), #10568, .F. ) ;
#80211=VECTOR ( 'NONE', #48050, 1000.000000000000000 ) ;
#80212=AXIS2_PLACEMENT_3D ( 'NONE', #11811, #16076, #36455 ) ;
#80216=CARTESIAN_POINT ( 'NONE',  ( 4.171830600776445408, -14.24070752338413470, 4.000000000000000000 ) ) ;
#80217=ORIENTED_EDGE ( 'NONE', *, *, #74764, .F. ) ;
#80218=DIRECTION ( 'NONE',  ( -0.7071067811865486830, -0.7071067811865464625, 0.000000000000000000 ) ) ;
#80219=ORIENTED_EDGE ( 'NONE', *, *, #43514, .T. ) ;
#80221=AXIS2_PLACEMENT_3D ( 'NONE', #141219, #76724, #133239 ) ;
#80222=CARTESIAN_POINT ( 'NONE',  ( -33.33010218547244108, 17.25929247661554555, 19.83885114516079184 ) ) ;
#80223=ORIENTED_EDGE ( 'NONE', *, *, #139126, .F. ) ;
#80224=CARTESIAN_POINT ( 'NONE',  ( -7.499999999999944045, 13.46639925780212366, 5.000000000000000000 ) ) ;
#80225=LINE ( 'NONE', #114919, #2025 ) ;
#80227=VERTEX_POINT ( 'NONE', #64268 ) ;
#80228=PLANE ( 'NONE',  #101267 ) ;
#80229=ORIENTED_EDGE ( 'NONE', *, *, #69846, .T. ) ;
#80230=ORIENTED_EDGE ( 'NONE', *, *, #55281, .T. ) ;
#80231=VERTEX_POINT ( 'NONE', #99013 ) ;
#80232=EDGE_CURVE ( 'NONE', #60276, #73694, #43945, .T. ) ;
#80233=DIRECTION ( 'NONE',  ( -0.7071067811865487940, 0.7071067811865463515, 0.000000000000000000 ) ) ;
#80234=CARTESIAN_POINT ( 'NONE',  ( -5.999999999999952927, 14.96639925780211478, 5.000000000000000000 ) ) ;
#80235=DIRECTION ( 'NONE',  ( -0.6830127018922181881, 0.6830127018922202975, -0.2588190451025214056 ) ) ;
#80238=EDGE_CURVE ( 'NONE', #82756, #74817, #97588, .T. ) ;
#80240=CARTESIAN_POINT ( 'NONE',  ( -19.49999999999986855, -12.66682484999668112, -0.6294897503864391730 ) ) ;
#80241=AXIS2_PLACEMENT_3D ( 'NONE', #136894, #72400, #113713 ) ;
#80244=FACE_OUTER_BOUND ( 'NONE', #34165, .T. ) ;
#80245=VERTEX_POINT ( 'NONE', #66421 ) ;
#80246=ORIENTED_EDGE ( 'NONE', *, *, #121943, .T. ) ;
#80247=EDGE_CURVE ( 'NONE', #120012, #91787, #45401, .T. ) ;
#80250=PLANE ( 'NONE',  #71911 ) ;
#80251=VECTOR ( 'NONE', #40024, 999.9999999999998863 ) ;
#80253=CARTESIAN_POINT ( 'NONE',  ( -14.99451991528749595, 28.92564299267948513, 4.000000000000000000 ) ) ;
#80254=CARTESIAN_POINT ( 'NONE',  ( 9.278254515685670611, 8.259292476615634371, 11.78515199841152850 ) ) ;
#80255=FACE_OUTER_BOUND ( 'NONE', #37712, .T. ) ;
#80257=ADVANCED_FACE ( 'NONE', ( #107746 ), #121486, .F. ) ;
#80258=PLANE ( 'NONE',  #141284 ) ;
#80259=CARTESIAN_POINT ( 'NONE',  ( 18.18398860626898994, 28.73617430169800002, 5.000000000000000000 ) ) ;
#80260=CARTESIAN_POINT ( 'NONE',  ( 34.42499999999998295, 21.72500000000000142, 5.000000000000000000 ) ) ;
#80261=VECTOR ( 'NONE', #142485, 999.9999999999998863 ) ;
#80262=ORIENTED_EDGE ( 'NONE', *, *, #50050, .T. ) ;
#80263=VERTEX_POINT ( 'NONE', #132420 ) ;
#80264=DIRECTION ( 'NONE',  ( -0.7071067811865486830, -0.7071067811865464625, 0.000000000000000000 ) ) ;
#80265=CARTESIAN_POINT ( 'NONE',  ( 12.48921356237309155, -27.52281430457064104, 5.000000000000000000 ) ) ;
#80266=ORIENTED_EDGE ( 'NONE', *, *, #119211, .F. ) ;
#80267=ADVANCED_FACE ( 'NONE', ( #98333 ), #65001, .F. ) ;
#80268=CARTESIAN_POINT ( 'NONE',  ( -26.20710678118636139, 18.75929247661552068, 5.000000000000000000 ) ) ;
#80269=EDGE_CURVE ( 'NONE', #126646, #59525, #88897, .T. ) ;
#80270=VERTEX_POINT ( 'NONE', #119332 ) ;
#80271=FACE_OUTER_BOUND ( 'NONE', #113861, .T. ) ;
#80272=ORIENTED_EDGE ( 'NONE', *, *, #123807, .F. ) ;
#80273=LINE ( 'NONE', #123773, #125385 ) ;
#80274=ORIENTED_EDGE ( 'NONE', *, *, #68569, .F. ) ;
#80276=CARTESIAN_POINT ( 'NONE',  ( 45.18398860626900415, 28.73617430169818832, 5.000000000000000000 ) ) ;
#80277=AXIS2_PLACEMENT_3D ( 'NONE', #77856, #56859, #110448 ) ;
#80279=CARTESIAN_POINT ( 'NONE',  ( 42.18398860626899705, 28.73617430169816700, 5.000000000000000000 ) ) ;
#80280=CARTESIAN_POINT ( 'NONE',  ( 13.19018167574440348, -18.74070752338408852, 7.910009926591477836 ) ) ;
#80281=VERTEX_POINT ( 'NONE', #21480 ) ;
#80283=DIRECTION ( 'NONE',  ( 0.6830127018922181881, 0.6830127018922202975, -0.2588190451025214056 ) ) ;
#80284=DIRECTION ( 'NONE',  ( -0.7071067811865486830, -0.7071067811865464625, 0.000000000000000000 ) ) ;
#80285=DIRECTION ( 'NONE',  ( -0.000000000000000000, 0.3543493200069153248, 0.9351131265310292928 ) ) ;
#80288=LINE ( 'NONE', #25150, #10723 ) ;
#80290=EDGE_CURVE ( 'NONE', #113241, #67529, #130968, .T. ) ;
#80291=PLANE ( 'NONE',  #39824 ) ;
#80292=ORIENTED_EDGE ( 'NONE', *, *, #109651, .T. ) ;
#80293=EDGE_CURVE ( 'NONE', #49354, #51668, #9872, .T. ) ;
#80294=AXIS2_PLACEMENT_3D ( 'NONE', #142575, #42564, #63605 ) ;
#80296=DIRECTION ( 'NONE',  ( -0.7071067811865486830, -0.7071067811865464625, 0.000000000000000000 ) ) ;
#80297=CARTESIAN_POINT ( 'NONE',  ( 8.999999999999944933, -7.447814304570754551, 5.000000000000000000 ) ) ;
#80298=LINE ( 'NONE', #33926, #72431 ) ;
#80299=CARTESIAN_POINT ( 'NONE',  ( -10.03340032343016652, 6.759292476615645917, 12.28218704918519855 ) ) ;
#80300=VERTEX_POINT ( 'NONE', #130254 ) ;
#80301=CARTESIAN_POINT ( 'NONE',  ( 53.99451991528749062, 28.92564299267975869, 4.000000000000000000 ) ) ;
#80302=CARTESIAN_POINT ( 'NONE',  ( 8.999999999999937828, 20.96639925780204905, 5.000000000000000000 ) ) ;
#80303=EDGE_CURVE ( 'NONE', #17021, #10403, #142554, .T. ) ;
#80305=ORIENTED_EDGE ( 'NONE', *, *, #86515, .F. ) ;
#80306=CARTESIAN_POINT ( 'NONE',  ( 48.48921356237309510, -27.52281430457089328, 5.000000000000000000 ) ) ;
#80309=CARTESIAN_POINT ( 'NONE',  ( -30.85181644961836867, 17.25929247661554200, 8.802941693769131604 ) ) ;
#80311=LINE ( 'NONE', #98638, #108501 ) ;
#80313=DIRECTION ( 'NONE',  ( -0.6830127018922181881, 0.6830127018922202975, -0.2588190451025214056 ) ) ;
#80314=CARTESIAN_POINT ( 'NONE',  ( -50.99451991528749062, 28.92564299267973738, 4.000000000000000000 ) ) ;
#80316=CARTESIAN_POINT ( 'NONE',  ( -3.183988606268992161, 28.73617430169789699, 5.000000000000000000 ) ) ;
#80317=VECTOR ( 'NONE', #8069, 1000.000000000000000 ) ;
#80318=ORIENTED_EDGE ( 'NONE', *, *, #50133, .F. ) ;
#80319=VERTEX_POINT ( 'NONE', #96848 ) ;
#80320=VERTEX_POINT ( 'NONE', #22160 ) ;
#80321=VECTOR ( 'NONE', #112893, 1000.000000000000000 ) ;
#80323=ORIENTED_EDGE ( 'NONE', *, *, #83126, .T. ) ;
#80324=FACE_OUTER_BOUND ( 'NONE', #17372, .T. ) ;
#80325=CARTESIAN_POINT ( 'NONE',  ( -2.816011393730999401, 28.73617430169785436, 5.000000000000000000 ) ) ;
#80326=LINE ( 'NONE', #34661, #129018 ) ;
#80327=AXIS2_PLACEMENT_3D ( 'NONE', #99511, #115370, #14679 ) ;
#80328=DIRECTION ( 'NONE',  ( 0.7071067811865487940, 0.7071067811865463515, 0.000000000000000000 ) ) ;
#80329=VERTEX_POINT ( 'NONE', #9110 ) ;
#80330=ADVANCED_FACE ( 'NONE', ( #76598 ), #55541, .F. ) ;
#80331=CARTESIAN_POINT ( 'NONE',  ( 14.09068777029287567, 6.496774105546209377, 4.000000000000000000 ) ) ;
#80332=DIRECTION ( 'NONE',  ( 0.7071067811865487940, -0.7071067811865463515, 0.000000000000000000 ) ) ;
#80333=CARTESIAN_POINT ( 'NONE',  ( 27.70701326429285061, -21.74070752338406365, 4.999753212805213565 ) ) ;
#80335=EDGE_LOOP ( 'NONE', ( #4976, #79658, #143049, #14186 ) ) ;
#80336=FACE_OUTER_BOUND ( 'NONE', #118203, .T. ) ;
#80337=CARTESIAN_POINT ( 'NONE',  ( -34.42500000000001137, -9.022814304570477617, 5.000000000000000000 ) ) ;
#80338=FACE_OUTER_BOUND ( 'NONE', #29270, .T. ) ;
#80339=VERTEX_POINT ( 'NONE', #23608 ) ;
#80340=EDGE_LOOP ( 'NONE', ( #68973, #24151, #136699 ) ) ;
#80341=DIRECTION ( 'NONE',  ( 0.6830127018922180770, -0.6830127018922204085, -0.2588190451025213501 ) ) ;
#80342=DIRECTION ( 'NONE',  ( 0.3543493200069162685, -0.000000000000000000, -0.9351131265310288487 ) ) ;
#80343=DIRECTION ( 'NONE',  ( 0.7071067811865487940, 0.7071067811865463515, -0.000000000000000000 ) ) ;
#80344=VECTOR ( 'NONE', #18096, 1000.000000000000227 ) ;
#80345=CARTESIAN_POINT ( 'NONE',  ( 57.48921356237308800, -27.52281430457095368, 5.000000000000000000 ) ) ;
#80346=CARTESIAN_POINT ( 'NONE',  ( -30.32816939922332367, -3.740707523384244837, 4.000000000000000000 ) ) ;
#80347=ADVANCED_FACE ( 'NONE', ( #100473 ), #34493, .T. ) ;
#80348=VECTOR ( 'NONE', #81579, 1000.000000000000227 ) ;
#80349=ORIENTED_EDGE ( 'NONE', *, *, #89352, .T. ) ;
#80350=ORIENTED_EDGE ( 'NONE', *, *, #5057, .T. ) ;
#80351=EDGE_CURVE ( 'NONE', #62423, #116876, #37355, .T. ) ;
#80352=FACE_OUTER_BOUND ( 'NONE', #17694, .T. ) ;
#80353=VERTEX_POINT ( 'NONE', #46852 ) ;
#80354=ORIENTED_EDGE ( 'NONE', *, *, #8912, .F. ) ;
#80355=CIRCLE ( 'NONE', #140540, 5.968999999999998529 ) ;
#80356=EDGE_CURVE ( 'NONE', #20015, #61417, #135938, .T. ) ;
#80357=EDGE_CURVE ( 'NONE', #94939, #93121, #35234, .T. ) ;
#80358=LINE ( 'NONE', #25951, #105325 ) ;
#80359=ORIENTED_EDGE ( 'NONE', *, *, #97317, .F. ) ;
#80360=DIRECTION ( 'NONE',  ( 0.7071067811865486830, -0.7071067811865464625, -0.000000000000000000 ) ) ;
#80361=CARTESIAN_POINT ( 'NONE',  ( 59.99451991528749772, 28.92564299267980132, 4.000000000000000000 ) ) ;
#80362=AXIS2_PLACEMENT_3D ( 'NONE', #100228, #876, #69775 ) ;
#80363=DIRECTION ( 'NONE',  ( 0.3543493200069162685, -0.000000000000000000, -0.9351131265310288487 ) ) ;
#80364=CARTESIAN_POINT ( 'NONE',  ( 5.510786437626906675, -27.52281430457051314, 5.000000000000000000 ) ) ;
#80365=ORIENTED_EDGE ( 'NONE', *, *, #83240, .T. ) ;
#80366=LINE ( 'NONE', #123865, #27884 ) ;
#80367=EDGE_CURVE ( 'NONE', #53073, #128957, #80869, .T. ) ;
#80368=VECTOR ( 'NONE', #50914, 1000.000000000000000 ) ;
#80369=EDGE_LOOP ( 'NONE', ( #51823, #71229, #10442, #36615 ) ) ;
#80370=FACE_OUTER_BOUND ( 'NONE', #95029, .T. ) ;
#80371=EDGE_LOOP ( 'NONE', ( #107777, #83595, #129372, #46969 ) ) ;
#80372=ADVANCED_FACE ( 'NONE', ( #45400 ), #14867, .F. ) ;
#80373=ORIENTED_EDGE ( 'NONE', *, *, #57092, .F. ) ;
#80374=CARTESIAN_POINT ( 'NONE',  ( -39.29974487139159578, -27.71228299555233576, 4.000000000000000000 ) ) ;
#80375=ORIENTED_EDGE ( 'NONE', *, *, #33517, .T. ) ;
#80376=ORIENTED_EDGE ( 'NONE', *, *, #65723, .T. ) ;
#80377=CARTESIAN_POINT ( 'NONE',  ( 19.49999999999986500, 15.05218569542901541, 5.000000000000000000 ) ) ;
#80378=ORIENTED_EDGE ( 'NONE', *, *, #131895, .F. ) ;
#80379=EDGE_CURVE ( 'NONE', #49858, #13267, #68572, .T. ) ;
#80380=DIRECTION ( 'NONE',  ( -0.3543493200069162685, -0.000000000000000000, -0.9351131265310288487 ) ) ;
#80381=DIRECTION ( 'NONE',  ( 0.7071067811865486830, -0.7071067811865464625, -0.000000000000000000 ) ) ;
#80382=AXIS2_PLACEMENT_3D ( 'NONE', #84449, #114189, #17029 ) ;
#80385=CARTESIAN_POINT ( 'NONE',  ( 24.66331758004193375, 1.142935889642021863, 4.329525704382053419 ) ) ;
#80386=CARTESIAN_POINT ( 'NONE',  ( -47.99451991528749062, 28.92564299267971251, 4.000000000000000000 ) ) ;
#80387=ADVANCED_FACE ( 'NONE', ( #114183 ), #1806, .T. ) ;
#80390=ORIENTED_EDGE ( 'NONE', *, *, #24189, .F. ) ;
#80391=PLANE ( 'NONE',  #66616 ) ;
#80392=ORIENTED_EDGE ( 'NONE', *, *, #24266, .F. ) ;
#80393=ORIENTED_EDGE ( 'NONE', *, *, #48883, .F. ) ;
#80394=EDGE_CURVE ( 'NONE', #1058, #131599, #67879, .T. ) ;
#80395=DIRECTION ( 'NONE',  ( -0.000000000000000000, -0.3543493200069152693, 0.9351131265310292928 ) ) ;
#80396=VERTEX_POINT ( 'NONE', #3269 ) ;
#80397=CARTESIAN_POINT ( 'NONE',  ( -19.49999999999986500, 15.43112307739202826, 4.000000000000000000 ) ) ;
#80399=LINE ( 'NONE', #4166, #136637 ) ;
#80401=EDGE_CURVE ( 'NONE', #131572, #60798, #3944, .T. ) ;
#80402=ORIENTED_EDGE ( 'NONE', *, *, #38960, .T. ) ;
#80403=LINE ( 'NONE', #36861, #127395 ) ;
#80404=ORIENTED_EDGE ( 'NONE', *, *, #111131, .T. ) ;
#80405=VECTOR ( 'NONE', #22860, 999.9999999999998863 ) ;
#80406=VECTOR ( 'NONE', #69472, 1000.000000000000000 ) ;
#80407=CARTESIAN_POINT ( 'NONE',  ( 5.510786437626906675, -27.52281430457051314, 5.000000000000000000 ) ) ;
#80408=ADVANCED_FACE ( 'NONE', ( #24326 ), #124354, .F. ) ;
#80411=ORIENTED_EDGE ( 'NONE', *, *, #89215, .T. ) ;
#80413=DIRECTION ( 'NONE',  ( -0.7071067811865486830, -0.7071067811865464625, 0.000000000000000000 ) ) ;
#80414=VERTEX_POINT ( 'NONE', #90283 ) ;
#80415=EDGE_LOOP ( 'NONE', ( #13838, #32242, #69858, #3368 ) ) ;
#80416=ORIENTED_EDGE ( 'NONE', *, *, #105471, .F. ) ;
#80417=LINE ( 'NONE', #102871, #51876 ) ;
#80418=PLANE ( 'NONE',  #118088 ) ;
#80419=VECTOR ( 'NONE', #67667, 1000.000000000000227 ) ;
#80420=LINE ( 'NONE', #68835, #28866 ) ;
#80421=DIRECTION ( 'NONE',  ( -0.6830127018922180770, -0.6830127018922204085, -0.2588190451025213501 ) ) ;
#80422=ORIENTED_EDGE ( 'NONE', *, *, #94440, .F. ) ;
#80423=DIRECTION ( 'NONE',  ( 0.3543493200069162685, -0.000000000000000000, -0.9351131265310288487 ) ) ;
#80424=DIRECTION ( 'NONE',  ( 0.000000000000000000, -1.000000000000000000, 0.000000000000000000 ) ) ;
#80425=ADVANCED_FACE ( 'NONE', ( #12004 ), #113457, .F. ) ;
#80426=CARTESIAN_POINT ( 'NONE',  ( -1.499999999999987566, -10.04351517176478659, -1.623559851933826570 ) ) ;
#80427=DIRECTION ( 'NONE',  ( -0.000000000000000000, 0.000000000000000000, 1.000000000000000000 ) ) ;
#80428=ORIENTED_EDGE ( 'NONE', *, *, #111131, .F. ) ;
#80429=CARTESIAN_POINT ( 'NONE',  ( 10.49999999999993072, -7.912538124160676922, 4.000000000000000000 ) ) ;
#80432=EDGE_LOOP ( 'NONE', ( #72913, #132220, #5508, #96726 ) ) ;
#80433=ORIENTED_EDGE ( 'NONE', *, *, #25782, .F. ) ;
#80434=EDGE_CURVE ( 'NONE', #65772, #17436, #35949, .T. ) ;
#80435=CARTESIAN_POINT ( 'NONE',  ( 7.499999999999954703, 19.46639925780207037, 5.000000000000000000 ) ) ;
#80436=LINE ( 'NONE', #27434, #34447 ) ;
#80437=AXIS2_PLACEMENT_3D ( 'NONE', #43121, #77193, #86632 ) ;
#80438=ORIENTED_EDGE ( 'NONE', *, *, #94300, .T. ) ;
#80439=LINE ( 'NONE', #23905, #11937 ) ;
#80441=DIRECTION ( 'NONE',  ( 1.000000000000000000, 0.000000000000000000, 0.000000000000000000 ) ) ;
#80442=DIRECTION ( 'NONE',  ( -0.7071067811865486830, -0.7071067811865464625, 0.000000000000000000 ) ) ;
#80443=VECTOR ( 'NONE', #78273, 1000.000000000000000 ) ;
#80444=DIRECTION ( 'NONE',  ( -0.7071067811865486830, -0.7071067811865464625, 0.000000000000000000 ) ) ;
#80445=CARTESIAN_POINT ( 'NONE',  ( -8.816011393731004731, 28.73617430169781173, 5.000000000000000000 ) ) ;
#80446=DIRECTION ( 'NONE',  ( 0.6830127018922180770, -0.6830127018922204085, -0.2588190451025213501 ) ) ;
#80447=CARTESIAN_POINT ( 'NONE',  ( -42.18398860626899705, 28.73617430169816700, 5.000000000000000000 ) ) ;
#80448=EDGE_CURVE ( 'NONE', #84277, #76846, #35236, .T. ) ;
#80449=DIRECTION ( 'NONE',  ( -0.7071067811865486830, 0.7071067811865464625, 0.000000000000000000 ) ) ;
#80450=CARTESIAN_POINT ( 'NONE',  ( 23.20666063542136115, 21.75929247661548871, 4.998822639870701856 ) ) ;
#80452=CARTESIAN_POINT ( 'NONE',  ( -0.2997448713915885632, -27.71228299555206220, 4.000000000000000000 ) ) ;
#80453=VECTOR ( 'NONE', #125951, 1000.000000000000000 ) ;
#80454=FACE_OUTER_BOUND ( 'NONE', #27333, .T. ) ;
#80455=CARTESIAN_POINT ( 'NONE',  ( -17.69668852761918032, -22.22500000000000142, 11.52845124498734464 ) ) ;
#80456=PLANE ( 'NONE',  #68733 ) ;
#80458=VERTEX_POINT ( 'NONE', #12721 ) ;
#80460=ORIENTED_EDGE ( 'NONE', *, *, #139424, .T. ) ;
#80461=EDGE_LOOP ( 'NONE', ( #81708, #121631, #5172, #30462 ) ) ;
#80462=ADVANCED_FACE ( 'NONE', ( #14149 ), #102621, .F. ) ;
#80463=ORIENTED_EDGE ( 'NONE', *, *, #114572, .T. ) ;
#80464=VECTOR ( 'NONE', #66028, 1000.000000000000000 ) ;
#80465=DIRECTION ( 'NONE',  ( 0.6830127018922180770, -0.6830127018922204085, -0.2588190451025213501 ) ) ;
#80466=DIRECTION ( 'NONE',  ( 0.7071067811865487940, -0.7071067811865463515, 0.000000000000000000 ) ) ;
#80468=ORIENTED_EDGE ( 'NONE', *, *, #140418, .T. ) ;
#80469=DIRECTION ( 'NONE',  ( 1.000000000000000000, 0.000000000000000000, 0.000000000000000000 ) ) ;
#80470=CARTESIAN_POINT ( 'NONE',  ( -35.99451991528749772, 28.92564299267963079, 4.000000000000000000 ) ) ;
#80471=CARTESIAN_POINT ( 'NONE',  ( -30.48921356237309510, -27.52281430457076894, 5.000000000000000000 ) ) ;
#80473=EDGE_CURVE ( 'NONE', #142250, #123516, #49681, .T. ) ;
#80475=EDGE_CURVE ( 'NONE', #26874, #81201, #26471, .T. ) ;
#80476=DIRECTION ( 'NONE',  ( 0.7071067811865486830, -0.7071067811865464625, -0.000000000000000000 ) ) ;
#80477=CARTESIAN_POINT ( 'NONE',  ( -23.99999999999983302, -5.527737879153217015, -7.983877177622316523 ) ) ;
#80478=LINE ( 'NONE', #79072, #24397 ) ;
#80479=CARTESIAN_POINT ( 'NONE',  ( 1.734723475976807094E-15, -3.033600742197708477, 5.000000000000000000 ) ) ;
#80480=CARTESIAN_POINT ( 'NONE',  ( 34.47516574401890210, 9.028067341115718847, 4.998110765256834398 ) ) ;
#80481=CARTESIAN_POINT ( 'NONE',  ( -20.29289321881331531, 17.25929247661554200, 5.000000000000000000 ) ) ;
#80483=VERTEX_POINT ( 'NONE', #103993 ) ;
#80484=VERTEX_POINT ( 'NONE', #138818 ) ;
#80487=VERTEX_POINT ( 'NONE', #93859 ) ;
#80488=EDGE_CURVE ( 'NONE', #127894, #26964, #126476, .T. ) ;
#80490=LINE ( 'NONE', #69623, #142681 ) ;
#80491=ADVANCED_FACE ( 'NONE', ( #48953 ), #93153, .F. ) ;
#80492=DIRECTION ( 'NONE',  ( -0.7071067811865486830, -0.7071067811865464625, -0.000000000000000000 ) ) ;
#80495=ORIENTED_EDGE ( 'NONE', *, *, #137828, .T. ) ;
#80496=ORIENTED_EDGE ( 'NONE', *, *, #67297, .F. ) ;
#80497=CARTESIAN_POINT ( 'NONE',  ( 4.499999999999972466, 6.277155672890274651, -3.510561720658952556 ) ) ;
#80498=PLANE ( 'NONE',  #98691 ) ;
#80499=AXIS2_PLACEMENT_3D ( 'NONE', #120830, #62924, #20081 ) ;
#80500=VERTEX_POINT ( 'NONE', #138088 ) ;
#80501=ORIENTED_EDGE ( 'NONE', *, *, #44927, .T. ) ;
#80502=ORIENTED_EDGE ( 'NONE', *, *, #45579, .F. ) ;
#80503=DIRECTION ( 'NONE',  ( 1.000000000000000000, 0.000000000000000000, 0.000000000000000000 ) ) ;
#80504=PLANE ( 'NONE',  #41534 ) ;
#80505=VECTOR ( 'NONE', #93532, 1000.000000000000000 ) ;
#80506=VECTOR ( 'NONE', #61136, 1000.000000000000000 ) ;
#80507=VECTOR ( 'NONE', #15020, 1000.000000000000000 ) ;
#80510=ORIENTED_EDGE ( 'NONE', *, *, #113742, .F. ) ;
#80511=ORIENTED_EDGE ( 'NONE', *, *, #647, .F. ) ;
#80512=EDGE_CURVE ( 'NONE', #70831, #21420, #38076, .T. ) ;
#80514=ORIENTED_EDGE ( 'NONE', *, *, #78858, .T. ) ;
#80515=ORIENTED_EDGE ( 'NONE', *, *, #111717, .T. ) ;
#80516=VECTOR ( 'NONE', #9100, 1000.000000000000000 ) ;
#80517=EDGE_CURVE ( 'NONE', #77643, #16581, #137385, .T. ) ;
#80518=ADVANCED_FACE ( 'NONE', ( #105438 ), #72160, .F. ) ;
#80519=FACE_OUTER_BOUND ( 'NONE', #85421, .T. ) ;
#80521=ORIENTED_EDGE ( 'NONE', *, *, #43023, .F. ) ;
#80522=PLANE ( 'NONE',  #99272 ) ;
#80523=DIRECTION ( 'NONE',  ( 0.7071067811865487940, 0.7071067811865463515, 0.000000000000000000 ) ) ;
#80524=PLANE ( 'NONE',  #60000 ) ;
#80525=ADVANCED_FACE ( 'NONE', ( #27170 ), #71412, .T. ) ;
#80526=DIRECTION ( 'NONE',  ( -0.6830127018922180770, -0.6830127018922204085, -0.2588190451025213501 ) ) ;
#80527=FACE_BOUND ( 'NONE', #105627, .T. ) ;
#80528=EDGE_CURVE ( 'NONE', #98083, #103858, #54697, .T. ) ;
#80529=ORIENTED_EDGE ( 'NONE', *, *, #29114, .T. ) ;
#80533=EDGE_CURVE ( 'NONE', #108682, #46312, #127942, .T. ) ;
#80534=ORIENTED_EDGE ( 'NONE', *, *, #3640, .F. ) ;
#80535=FACE_OUTER_BOUND ( 'NONE', #48174, .T. ) ;
#80536=ORIENTED_EDGE ( 'NONE', *, *, #913, .F. ) ;
#80537=AXIS2_PLACEMENT_3D ( 'NONE', #66106, #35634, #32763 ) ;
#80538=ORIENTED_EDGE ( 'NONE', *, *, #102336, .F. ) ;
#80539=ORIENTED_EDGE ( 'NONE', *, *, #60175, .F. ) ;
#80541=EDGE_CURVE ( 'NONE', #73668, #77753, #70488, .T. ) ;
#80543=ORIENTED_EDGE ( 'NONE', *, *, #125346, .T. ) ;
#80544=EDGE_CURVE ( 'NONE', #121977, #3709, #101627, .T. ) ;
#80545=CARTESIAN_POINT ( 'NONE',  ( -48.48921356237309510, -27.52281430457089328, 5.000000000000000000 ) ) ;
#80547=DIRECTION ( 'NONE',  ( -0.6830127018922181881, 0.6830127018922202975, -0.2588190451025214056 ) ) ;
#80548=VERTEX_POINT ( 'NONE', #81338 ) ;
#80549=CARTESIAN_POINT ( 'NONE',  ( 2.999999999999983569, 18.08204922493373346, 0.9627537363044802454 ) ) ;
#80552=PLANE ( 'NONE',  #120938 ) ;
#80553=LINE ( 'NONE', #71822, #69147 ) ;
#80554=DIRECTION ( 'NONE',  ( -0.3543493200069162685, -0.000000000000000000, -0.9351131265310288487 ) ) ;
#80555=PLANE ( 'NONE',  #80711 ) ;
#80557=EDGE_LOOP ( 'NONE', ( #13294, #9635, #116115 ) ) ;
#80558=ORIENTED_EDGE ( 'NONE', *, *, #73598, .T. ) ;
#80559=ADVANCED_FACE ( 'NONE', ( #82066 ), #80615, .T. ) ;
#80560=ORIENTED_EDGE ( 'NONE', *, *, #89007, .F. ) ;
#80561=ORIENTED_EDGE ( 'NONE', *, *, #123921, .T. ) ;
#80563=VERTEX_POINT ( 'NONE', #113935 ) ;
#80564=EDGE_LOOP ( 'NONE', ( #104530, #21714, #56848, #96391 ) ) ;
#80567=ORIENTED_EDGE ( 'NONE', *, *, #68898, .F. ) ;
#80569=FACE_OUTER_BOUND ( 'NONE', #135939, .T. ) ;
#80570=ORIENTED_EDGE ( 'NONE', *, *, #41668, .F. ) ;
#80571=FACE_OUTER_BOUND ( 'NONE', #34778, .T. ) ;
#80572=EDGE_CURVE ( 'NONE', #70280, #76991, #14626, .T. ) ;
#80575=ORIENTED_EDGE ( 'NONE', *, *, #77776, .T. ) ;
#80577=CARTESIAN_POINT ( 'NONE',  ( 14.35681257248253040, -20.24070752338407431, 21.22881796311216362 ) ) ;
#80578=AXIS2_PLACEMENT_3D ( 'NONE', #75358, #64467, #44733 ) ;
#80580=DIRECTION ( 'NONE',  ( -0.7071067811865486830, -0.7071067811865464625, 0.000000000000000000 ) ) ;
#80581=ORIENTED_EDGE ( 'NONE', *, *, #11572, .T. ) ;
#80583=ORIENTED_EDGE ( 'NONE', *, *, #109016, .T. ) ;
#80585=FACE_OUTER_BOUND ( 'NONE', #122227, .T. ) ;
#80587=DIRECTION ( 'NONE',  ( -0.7071067811865486830, -0.7071067811865464625, -0.000000000000000000 ) ) ;
#80588=EDGE_CURVE ( 'NONE', #92161, #137268, #92165, .T. ) ;
#80589=CARTESIAN_POINT ( 'NONE',  ( 27.48921356237309155, -27.52281430457074762, 5.000000000000000000 ) ) ;
#80591=ORIENTED_EDGE ( 'NONE', *, *, #89395, .T. ) ;
#80593=CARTESIAN_POINT ( 'NONE',  ( 18.00548008471250583, 28.92564299267925776, 4.000000000000000000 ) ) ;
#80594=DIRECTION ( 'NONE',  ( 1.000000000000000000, 0.000000000000000000, 0.000000000000000000 ) ) ;
#80596=PLANE ( 'NONE',  #136924 ) ;
#80597=LINE ( 'NONE', #30491, #5283 ) ;
#80598=ORIENTED_EDGE ( 'NONE', *, *, #132217, .T. ) ;
#80599=VECTOR ( 'NONE', #17550, 999.9999999999998863 ) ;
#80600=DIRECTION ( 'NONE',  ( 0.7071067811865487940, -0.7071067811865463515, 0.000000000000000000 ) ) ;
#80601=ORIENTED_EDGE ( 'NONE', *, *, #125007, .F. ) ;
#80602=EDGE_LOOP ( 'NONE', ( #68014, #55739, #112835, #137946 ) ) ;
#80603=LINE ( 'NONE', #11726, #91276 ) ;
#80605=VECTOR ( 'NONE', #74117, 1000.000000000000227 ) ;
#80606=VERTEX_POINT ( 'NONE', #111804 ) ;
#80607=VECTOR ( 'NONE', #69672, 1000.000000000000227 ) ;
#80608=DIRECTION ( 'NONE',  ( 0.6830127018922180770, -0.6830127018922204085, -0.2588190451025213501 ) ) ;
#80609=ORIENTED_EDGE ( 'NONE', *, *, #135953, .T. ) ;
#80610=CARTESIAN_POINT ( 'NONE',  ( -72.18398860626899705, 28.73617430169837661, 5.000000000000000000 ) ) ;
#80611=DIRECTION ( 'NONE',  ( -0.7071067811865486830, -0.7071067811865464625, 0.000000000000000000 ) ) ;
#80612=EDGE_CURVE ( 'NONE', #45041, #60739, #12470, .T. ) ;
#80614=CARTESIAN_POINT ( 'NONE',  ( -78.48921356237309510, -27.52281430457109934, 5.000000000000000000 ) ) ;
#80615=PLANE ( 'NONE',  #84182 ) ;
#80616=DIRECTION ( 'NONE',  ( -0.6830127018922180770, -0.6830127018922204085, -0.2588190451025213501 ) ) ;
#80617=FACE_OUTER_BOUND ( 'NONE', #63662, .T. ) ;
#80618=CARTESIAN_POINT ( 'NONE',  ( 0.000000000000000000, 0.000000000000000000, 5.000000000000000000 ) ) ;
#80619=VERTEX_POINT ( 'NONE', #69027 ) ;
#80620=ORIENTED_EDGE ( 'NONE', *, *, #62911, .F. ) ;
#80621=ORIENTED_EDGE ( 'NONE', *, *, #32548, .F. ) ;
#80623=ORIENTED_EDGE ( 'NONE', *, *, #6430, .T. ) ;
#80626=FACE_OUTER_BOUND ( 'NONE', #93501, .T. ) ;
#80628=VERTEX_POINT ( 'NONE', #125547 ) ;
#80629=CARTESIAN_POINT ( 'NONE',  ( -36.48921356237310221, -27.52281430457080802, 5.000000000000000000 ) ) ;
#80631=CARTESIAN_POINT ( 'NONE',  ( 25.49999999999982236, 18.43112307739199451, 4.000000000000000000 ) ) ;
#80632=CARTESIAN_POINT ( 'NONE',  ( -34.92500000000001137, 20.81665438641021382, 4.500000000000000888 ) ) ;
#80634=EDGE_CURVE ( 'NONE', #130061, #80908, #46598, .T. ) ;
#80635=ORIENTED_EDGE ( 'NONE', *, *, #94860, .F. ) ;
#80636=CARTESIAN_POINT ( 'NONE',  ( 25.01899999999999835, 3.174999999999997158, 5.000000000000000000 ) ) ;
#80638=VECTOR ( 'NONE', #88399, 999.9999999999998863 ) ;
#80640=DIRECTION ( 'NONE',  ( -0.3543493200069162685, -0.000000000000000000, -0.9351131265310288487 ) ) ;
#80641=CARTESIAN_POINT ( 'NONE',  ( 14.53839644629420569, -9.740707523384173783, 17.74957260769614109 ) ) ;
#80642=CARTESIAN_POINT ( 'NONE',  ( 33.29974487139158867, -27.71228299555229313, 4.000000000000000000 ) ) ;
#80643=FACE_OUTER_BOUND ( 'NONE', #135132, .T. ) ;
#80644=EDGE_CURVE ( 'NONE', #46174, #80908, #114635, .T. ) ;
#80646=ADVANCED_FACE ( 'NONE', ( #34976 ), #45855, .T. ) ;
#80647=DIRECTION ( 'NONE',  ( -0.000000000000000000, 0.3543493200069153248, 0.9351131265310292928 ) ) ;
#80648=CARTESIAN_POINT ( 'NONE',  ( 36.18398860626899705, 28.73617430169812437, 5.000000000000000000 ) ) ;
#80649=ORIENTED_EDGE ( 'NONE', *, *, #113862, .T. ) ;
#80650=ORIENTED_EDGE ( 'NONE', *, *, #64943, .T. ) ;
#80653=ORIENTED_EDGE ( 'NONE', *, *, #24389, .F. ) ;
#80654=ADVANCED_FACE ( 'NONE', ( #126249 ), #137126, .F. ) ;
#80655=DIRECTION ( 'NONE',  ( -0.7071067811865487940, 0.7071067811865463515, 0.000000000000000000 ) ) ;
#80656=DIRECTION ( 'NONE',  ( 0.7071067811865487940, 0.7071067811865463515, -0.000000000000000000 ) ) ;
#80657=ORIENTED_EDGE ( 'NONE', *, *, #89799, .F. ) ;
#80659=FACE_OUTER_BOUND ( 'NONE', #73794, .T. ) ;
#80660=DIRECTION ( 'NONE',  ( -0.000000000000000000, -0.3543493200069152693, 0.9351131265310292928 ) ) ;
#80661=VECTOR ( 'NONE', #131590, 1000.000000000000000 ) ;
#80662=EDGE_CURVE ( 'NONE', #90647, #128697, #136395, .T. ) ;
#80664=EDGE_LOOP ( 'NONE', ( #141282, #29631, #61596, #86415 ) ) ;
#80665=LINE ( 'NONE', #38573, #57249 ) ;
#80666=ORIENTED_EDGE ( 'NONE', *, *, #11759, .F. ) ;
#80667=DIRECTION ( 'NONE',  ( -0.000000000000000000, 0.3543493200069153248, 0.9351131265310292928 ) ) ;
#80669=LINE ( 'NONE', #2336, #107885 ) ;
#80671=CARTESIAN_POINT ( 'NONE',  ( 8.510786437626906675, -27.52281430457049183, 5.000000000000000000 ) ) ;
#80672=ORIENTED_EDGE ( 'NONE', *, *, #47808, .T. ) ;
#80673=ORIENTED_EDGE ( 'NONE', *, *, #54062, .T. ) ;
#80674=DIRECTION ( 'NONE',  ( -0.6830127018922181881, 0.6830127018922202975, -0.2588190451025214056 ) ) ;
#80675=LINE ( 'NONE', #124161, #143414 ) ;
#80676=DIRECTION ( 'NONE',  ( -0.7071067811865487940, 0.7071067811865463515, -0.000000000000000000 ) ) ;
#80677=ADVANCED_FACE ( 'NONE', ( #124102 ), #37831, .F. ) ;
#80678=CARTESIAN_POINT ( 'NONE',  ( -34.49999999999975842, 10.46425560840038038, 4.994342998332163219 ) ) ;
#80679=CARTESIAN_POINT ( 'NONE',  ( -17.99451991528748351, 28.92564299267950645, 4.000000000000000000 ) ) ;
#80680=EDGE_CURVE ( 'NONE', #82809, #125587, #58181, .T. ) ;
#80681=VECTOR ( 'NONE', #120422, 1000.000000000000000 ) ;
#80683=CARTESIAN_POINT ( 'NONE',  ( 42.29974487139158157, -27.71228299555235708, 4.000000000000000000 ) ) ;
#80684=ADVANCED_FACE ( 'NONE', ( #122996 ), #79544, .F. ) ;
#80685=CARTESIAN_POINT ( 'NONE',  ( 29.29289321881325847, -12.74070752338415247, 5.000000000000000000 ) ) ;
#80686=ORIENTED_EDGE ( 'NONE', *, *, #49089, .T. ) ;
#80688=FACE_OUTER_BOUND ( 'NONE', #107253, .T. ) ;
#80689=ORIENTED_EDGE ( 'NONE', *, *, #78750, .F. ) ;
#80690=EDGE_CURVE ( 'NONE', #140203, #24994, #124416, .T. ) ;
#80691=EDGE_CURVE ( 'NONE', #19406, #22039, #57764, .T. ) ;
#80692=LINE ( 'NONE', #91560, #78960 ) ;
#80694=ORIENTED_EDGE ( 'NONE', *, *, #132041, .T. ) ;
#80695=CARTESIAN_POINT ( 'NONE',  ( 34.75611968250419181, 7.705650698523971442, 4.955485411084875835 ) ) ;
#80696=LINE ( 'NONE', #27005, #106389 ) ;
#80697=AXIS2_PLACEMENT_3D ( 'NONE', #74473, #18609, #21506 ) ;
#80699=EDGE_CURVE ( 'NONE', #7787, #10314, #113524, .T. ) ;
#80701=VECTOR ( 'NONE', #13424, 1000.000000000000000 ) ;
#80702=FACE_BOUND ( 'NONE', #86893, .T. ) ;
#80704=LINE ( 'NONE', #37915, #128981 ) ;
#80705=VECTOR ( 'NONE', #109988, 1000.000000000000000 ) ;
#80706=CARTESIAN_POINT ( 'NONE',  ( -9.792893218813388145, -5.240707523384232402, 5.000000000000000000 ) ) ;
#80707=LINE ( 'NONE', #27724, #59543 ) ;
#80710=ORIENTED_EDGE ( 'NONE', *, *, #78707, .F. ) ;
#80711=AXIS2_PLACEMENT_3D ( 'NONE', #2215, #101554, #70426 ) ;
#80712=VECTOR ( 'NONE', #139465, 1000.000000000000000 ) ;
#80713=LINE ( 'NONE', #25580, #35598 ) ;
#80716=ORIENTED_EDGE ( 'NONE', *, *, #133383, .T. ) ;
#80718=EDGE_LOOP ( 'NONE', ( #66464, #129369, #62673, #86489 ) ) ;
#80719=EDGE_CURVE ( 'NONE', #104365, #40167, #91103, .T. ) ;
#80720=CARTESIAN_POINT ( 'NONE',  ( 60.18398860626900415, 28.73617430169829490, 5.000000000000000000 ) ) ;
#80721=ORIENTED_EDGE ( 'NONE', *, *, #73489, .T. ) ;
#80722=CARTESIAN_POINT ( 'NONE',  ( -42.18398860626899705, 28.73617430169816700, 5.000000000000000000 ) ) ;
#80724=EDGE_CURVE ( 'NONE', #25800, #39048, #1185, .T. ) ;
#80726=VECTOR ( 'NONE', #81154, 1000.000000000000114 ) ;
#80727=LINE ( 'NONE', #69134, #31710 ) ;
#80728=FACE_OUTER_BOUND ( 'NONE', #121082, .T. ) ;
#80729=DIRECTION ( 'NONE',  ( -0.7071067811865486830, -0.7071067811865464625, 0.000000000000000000 ) ) ;
#80730=LINE ( 'NONE', #58302, #116462 ) ;
#80732=ORIENTED_EDGE ( 'NONE', *, *, #125985, .F. ) ;
#80733=AXIS2_PLACEMENT_3D ( 'NONE', #23162, #110881, #123953 ) ;
#80734=ORIENTED_EDGE ( 'NONE', *, *, #42917, .T. ) ;
#80736=CARTESIAN_POINT ( 'NONE',  ( 20.28769006033958178, -21.73547319004781642, 4.999917730833664642 ) ) ;
#80737=ORIENTED_EDGE ( 'NONE', *, *, #93864, .T. ) ;
#80738=AXIS2_PLACEMENT_3D ( 'NONE', #509, #133217, #33894 ) ;
#80739=ORIENTED_EDGE ( 'NONE', *, *, #72802, .T. ) ;
#80740=AXIS2_PLACEMENT_3D ( 'NONE', #103675, #91419, #15240 ) ;
#80741=ORIENTED_EDGE ( 'NONE', *, *, #111040, .F. ) ;
#80742=CARTESIAN_POINT ( 'NONE',  ( -19.49999999999986500, 9.127013188829483425, 4.802533355213530086 ) ) ;
#80744=VECTOR ( 'NONE', #69950, 999.9999999999998863 ) ;
#80745=DIRECTION ( 'NONE',  ( 1.000000000000000000, 0.000000000000000000, 0.000000000000000000 ) ) ;
#80747=PLANE ( 'NONE',  #60944 ) ;
#80749=DIRECTION ( 'NONE',  ( -0.000000000000000000, 0.3543493200069153248, 0.9351131265310292928 ) ) ;
#80750=ORIENTED_EDGE ( 'NONE', *, *, #130934, .F. ) ;
#80751=DIRECTION ( 'NONE',  ( 0.000000000000000000, -1.000000000000000000, 0.000000000000000000 ) ) ;
#80752=DIRECTION ( 'NONE',  ( 0.6830127018922181881, 0.6830127018922202975, -0.2588190451025214056 ) ) ;
#80753=DIRECTION ( 'NONE',  ( 0.7071067811865487940, 0.7071067811865463515, -0.000000000000000000 ) ) ;
#80754=VECTOR ( 'NONE', #90191, 999.9999999999998863 ) ;
#80755=DIRECTION ( 'NONE',  ( -0.7071067811865486830, -0.7071067811865464625, 0.000000000000000000 ) ) ;
#80756=ORIENTED_EDGE ( 'NONE', *, *, #83066, .F. ) ;
#80757=VERTEX_POINT ( 'NONE', #112821 ) ;
#80758=DIRECTION ( 'NONE',  ( -0.7071067811865487940, 0.7071067811865463515, 0.000000000000000000 ) ) ;
#80759=FACE_OUTER_BOUND ( 'NONE', #127257, .T. ) ;
#80760=VECTOR ( 'NONE', #44437, 1000.000000000000000 ) ;
#80761=DIRECTION ( 'NONE',  ( 0.7071067811865486830, -0.7071067811865464625, -0.000000000000000000 ) ) ;
#80762=ORIENTED_EDGE ( 'NONE', *, *, #53585, .T. ) ;
#80763=DIRECTION ( 'NONE',  ( -0.7071067811865487940, 0.7071067811865463515, -0.000000000000000000 ) ) ;
#80764=LINE ( 'NONE', #1707, #122782 ) ;
#80765=DIRECTION ( 'NONE',  ( -0.7071067811865486830, 0.7071067811865464625, 0.000000000000000000 ) ) ;
#80768=FACE_OUTER_BOUND ( 'NONE', #142081, .T. ) ;
#80769=DIRECTION ( 'NONE',  ( 0.7071067811865487940, 0.7071067811865463515, 0.000000000000000000 ) ) ;
#80771=LINE ( 'NONE', #24239, #25149 ) ;
#80772=VERTEX_POINT ( 'NONE', #135323 ) ;
#80773=VERTEX_POINT ( 'NONE', #80929 ) ;
#80774=CARTESIAN_POINT ( 'NONE',  ( 14.51078643762690490, -27.52281430457045275, 5.000000000000000000 ) ) ;
#80777=CARTESIAN_POINT ( 'NONE',  ( 21.48921356237309155, -27.52281430457070499, 5.000000000000000000 ) ) ;
#80778=FACE_OUTER_BOUND ( 'NONE', #73620, .T. ) ;
#80779=DIRECTION ( 'NONE',  ( 0.7071067811865487940, 0.7071067811865463515, 0.000000000000000000 ) ) ;
#80780=CARTESIAN_POINT ( 'NONE',  ( -21.48921356237309155, -27.52281430457070499, 5.000000000000000000 ) ) ;
#80781=ORIENTED_EDGE ( 'NONE', *, *, #130775, .F. ) ;
#80783=LINE ( 'NONE', #124982, #107156 ) ;
#80786=FACE_OUTER_BOUND ( 'NONE', #433, .T. ) ;
#80787=EDGE_CURVE ( 'NONE', #115169, #54350, #13478, .T. ) ;
#80788=CARTESIAN_POINT ( 'NONE',  ( -28.49999999999979750, -15.29013452822857033, 0.3645803511609698733 ) ) ;
#80790=DIRECTION ( 'NONE',  ( -0.7071067811865487940, 0.7071067811865463515, -0.000000000000000000 ) ) ;
#80791=ADVANCED_FACE ( 'NONE', ( #102684 ), #69340, .F. ) ;
#80792=EDGE_CURVE ( 'NONE', #57879, #23024, #101952, .T. ) ;
#80793=EDGE_LOOP ( 'NONE', ( #45161, #102937, #24618, #112590 ) ) ;
#80794=EDGE_CURVE ( 'NONE', #2255, #91343, #2616, .T. ) ;
#80797=VECTOR ( 'NONE', #26550, 1000.000000000000000 ) ;
#80798=VECTOR ( 'NONE', #75960, 1000.000000000000227 ) ;
#80799=LINE ( 'NONE', #90969, #57766 ) ;
#80800=CARTESIAN_POINT ( 'NONE',  ( 1.966599676569761534, 6.759292476615653023, 12.28218704918522519 ) ) ;
#80802=EDGE_CURVE ( 'NONE', #89781, #102633, #49746, .T. ) ;
#80803=DIRECTION ( 'NONE',  ( 0.7071067811865486830, -0.7071067811865464625, -0.000000000000000000 ) ) ;
#80804=PLANE ( 'NONE',  #108977 ) ;
#80807=ADVANCED_FACE ( 'NONE', ( #106198 ), #27962, .T. ) ;
#80808=EDGE_LOOP ( 'NONE', ( #87266, #105541, #32063, #126660 ) ) ;
#80809=ORIENTED_EDGE ( 'NONE', *, *, #114206, .F. ) ;
#80811=CARTESIAN_POINT ( 'NONE',  ( -48.48921356237309510, -27.52281430457089328, 5.000000000000000000 ) ) ;
#80813=VECTOR ( 'NONE', #60293, 999.9999999999998863 ) ;
#80814=CARTESIAN_POINT ( 'NONE',  ( -10.49999999999992717, 9.052185695429074030, 5.000000000000000000 ) ) ;
#80815=CARTESIAN_POINT ( 'NONE',  ( -84.18398860626899705, 28.73617430169846187, 5.000000000000000000 ) ) ;
#80818=EDGE_CURVE ( 'NONE', #73610, #89253, #83059, .T. ) ;
#80819=LINE ( 'NONE', #33754, #83090 ) ;
#80820=VERTEX_POINT ( 'NONE', #139616 ) ;
#80822=DIRECTION ( 'NONE',  ( 1.000000000000000000, 0.000000000000000000, 0.000000000000000000 ) ) ;
#80823=ADVANCED_FACE ( 'NONE', ( #104060 ), #38141, .F. ) ;
#80824=CARTESIAN_POINT ( 'NONE',  ( 22.49999999999984723, -7.912538124160680475, 4.000000000000000000 ) ) ;
#80825=CARTESIAN_POINT ( 'NONE',  ( 8.999999999999944933, -0.8619312979531862373, -5.102805207349806693 ) ) ;
#80828=DIRECTION ( 'NONE',  ( -0.7071067811865486830, -0.7071067811865464625, -0.000000000000000000 ) ) ;
#80829=EDGE_CURVE ( 'NONE', #7006, #94037, #70781, .T. ) ;
#80831=CARTESIAN_POINT ( 'NONE',  ( 26.29289321881327623, -15.74070752338411694, 5.000000000000000000 ) ) ;
#80833=DIRECTION ( 'NONE',  ( 0.6830127018922181881, 0.6830127018922202975, -0.2588190451025214056 ) ) ;
#80834=ORIENTED_EDGE ( 'NONE', *, *, #98369, .F. ) ;
#80837=VECTOR ( 'NONE', #138023, 1000.000000000000227 ) ;
#80838=CARTESIAN_POINT ( 'NONE',  ( -34.49999999999975842, -1.592773361805403853, -6.492772025301150052 ) ) ;
#80839=PLANE ( 'NONE',  #92880 ) ;
#80840=CIRCLE ( 'NONE', #92381, 5.968999999999998529 ) ;
#80843=DIRECTION ( 'NONE',  ( -0.3543493200069162685, -0.000000000000000000, -0.9351131265310288487 ) ) ;
#80844=ORIENTED_EDGE ( 'NONE', *, *, #108893, .T. ) ;
#80845=CARTESIAN_POINT ( 'NONE',  ( 2.816011393730999401, 28.73617430169785436, 5.000000000000000000 ) ) ;
#80847=FACE_OUTER_BOUND ( 'NONE', #28664, .T. ) ;
#80848=VECTOR ( 'NONE', #2674, 1000.000000000000000 ) ;
#80849=EDGE_CURVE ( 'NONE', #16022, #74522, #105499, .T. ) ;
#80850=LINE ( 'NONE', #35927, #140986 ) ;
#80851=ORIENTED_EDGE ( 'NONE', *, *, #50346, .T. ) ;
#80852=VERTEX_POINT ( 'NONE', #6875 ) ;
#80854=CARTESIAN_POINT ( 'NONE',  ( -32.93988928955960205, -9.740707523384180888, 10.89222023123388539 ) ) ;
#80855=ADVANCED_FACE ( 'NONE', ( #127260 ), #140294, .F. ) ;
#80856=DIRECTION ( 'NONE',  ( 0.7071067811865486830, -0.7071067811865464625, -0.000000000000000000 ) ) ;
#80857=LINE ( 'NONE', #125048, #133471 ) ;
#80858=ORIENTED_EDGE ( 'NONE', *, *, #24705, .F. ) ;
#80860=AXIS2_PLACEMENT_3D ( 'NONE', #76310, #31373, #87886 ) ;
#80861=CARTESIAN_POINT ( 'NONE',  ( -8.999999999999937828, -10.06887692260771416, 4.000000000000000000 ) ) ;
#80862=CARTESIAN_POINT ( 'NONE',  ( 6.707106781186507050, 5.259292476615661016, 5.000000000000000000 ) ) ;
#80863=EDGE_CURVE ( 'NONE', #7505, #40271, #71473, .T. ) ;
#80865=CARTESIAN_POINT ( 'NONE',  ( 5.524873872149501430, 14.25929247661557397, 9.797011795316649341 ) ) ;
#80866=ORIENTED_EDGE ( 'NONE', *, *, #13385, .F. ) ;
#80868=CYLINDRICAL_SURFACE ( 'NONE', #38687, 0.5000000000000004441 ) ;
#80869=LINE ( 'NONE', #70016, #139551 ) ;
#80870=ORIENTED_EDGE ( 'NONE', *, *, #131378, .F. ) ;
#80871=EDGE_CURVE ( 'NONE', #36504, #101734, #40298, .T. ) ;
#80872=FACE_BOUND ( 'NONE', #24574, .T. ) ;
#80873=LINE ( 'NONE', #66426, #29327 ) ;
#80874=DIRECTION ( 'NONE',  ( 1.000000000000000000, 0.000000000000000000, 0.000000000000000000 ) ) ;
#80876=CARTESIAN_POINT ( 'NONE',  ( -30.29974487139158867, -27.71228299555227537, 4.000000000000000000 ) ) ;
#80877=EDGE_CURVE ( 'NONE', #111536, #70500, #104805, .T. ) ;
#80879=ORIENTED_EDGE ( 'NONE', *, *, #91771, .T. ) ;
#80880=VERTEX_POINT ( 'NONE', #4716 ) ;
#80882=ORIENTED_EDGE ( 'NONE', *, *, #64279, .T. ) ;
#80883=EDGE_CURVE ( 'NONE', #41591, #38790, #62752, .T. ) ;
#80884=FACE_OUTER_BOUND ( 'NONE', #39724, .T. ) ;
#80885=FACE_OUTER_BOUND ( 'NONE', #96970, .T. ) ;
#80887=CARTESIAN_POINT ( 'NONE',  ( -32.01844734635648848, 18.75929247661553134, 20.33588619593450630 ) ) ;
#80888=ORIENTED_EDGE ( 'NONE', *, *, #106887, .F. ) ;
#80889=LINE ( 'NONE', #127214, #13591 ) ;
#80890=DIRECTION ( 'NONE',  ( 0.7071067811865487940, 0.7071067811865463515, -0.000000000000000000 ) ) ;
#80891=LINE ( 'NONE', #69304, #22999 ) ;
#80892=VECTOR ( 'NONE', #83389, 1000.000000000000000 ) ;
#80893=VECTOR ( 'NONE', #46766, 1000.000000000000000 ) ;
#80894=CARTESIAN_POINT ( 'NONE',  ( -33.32816939922329880, -0.7407075233842822515, 4.000000000000000000 ) ) ;
#80895=AXIS2_PLACEMENT_3D ( 'NONE', #100446, #21458, #109884 ) ;
#80896=ORIENTED_EDGE ( 'NONE', *, *, #99339, .F. ) ;
#80897=DIRECTION ( 'NONE',  ( 0.7071067811865487940, -0.7071067811865463515, 0.000000000000000000 ) ) ;
#80898=DIRECTION ( 'NONE',  ( 0.7071067811865487940, 0.7071067811865463515, -0.000000000000000000 ) ) ;
#80899=VECTOR ( 'NONE', #94052, 1000.000000000000000 ) ;
#80900=ORIENTED_EDGE ( 'NONE', *, *, #52142, .T. ) ;
#80901=ORIENTED_EDGE ( 'NONE', *, *, #3240, .T. ) ;
#80902=VERTEX_POINT ( 'NONE', #38843 ) ;
#80907=CYLINDRICAL_SURFACE ( 'NONE', #118919, 0.5000000000000004441 ) ;
#80908=VERTEX_POINT ( 'NONE', #82361 ) ;
#80909=CARTESIAN_POINT ( 'NONE',  ( -2.207106781186527478, 9.759292476615625489, 5.000000000000000000 ) ) ;
#80910=ORIENTED_EDGE ( 'NONE', *, *, #123216, .T. ) ;
#80913=AXIS2_PLACEMENT_3D ( 'NONE', #92313, #133711, #81495 ) ;
#80914=CARTESIAN_POINT ( 'NONE',  ( 29.99451991528749417, 28.92564299267958816, 4.000000000000000000 ) ) ;
#80915=VERTEX_POINT ( 'NONE', #6164 ) ;
#80916=VERTEX_POINT ( 'NONE', #50441 ) ;
#80917=( BOUNDED_CURVE ( )  B_SPLINE_CURVE ( 3, ( #132919, #78507, #133611, #98119 ),
 .UNSPECIFIED., .F., .F. ) 
 B_SPLINE_CURVE_WITH_KNOTS ( ( 4, 4 ),
 ( 1.208578181583236821, 1.359146454359402734 ),
 .UNSPECIFIED. ) 
 CURVE ( )  GEOMETRIC_REPRESENTATION_ITEM ( )  RATIONAL_B_SPLINE_CURVE ( ( 1.000000000000000000, 0.9981116584018963067, 0.9981116584018963067, 1.000000000000000000 ) ) 
 REPRESENTATION_ITEM ( '' )  );
#80918=EDGE_CURVE ( 'NONE', #32917, #36959, #115638, .T. ) ;
#80919=CARTESIAN_POINT ( 'NONE',  ( -1.499999999999982236, 12.05218569542904561, 5.000000000000000000 ) ) ;
#80920=LINE ( 'NONE', #57755, #120105 ) ;
#80921=CARTESIAN_POINT ( 'NONE',  ( -13.49999999999990585, -17.91344420646044000, 1.358650452708432654 ) ) ;
#80922=ORIENTED_EDGE ( 'NONE', *, *, #15329, .T. ) ;
#80923=AXIS2_PLACEMENT_3D ( 'NONE', #24817, #69060, #113240 ) ;
#80924=EDGE_CURVE ( 'NONE', #71113, #82851, #5465, .T. ) ;
#80925=CARTESIAN_POINT ( 'NONE',  ( -66.18398860626901126, 28.73617430169833753, 5.000000000000000000 ) ) ;
#80926=VERTEX_POINT ( 'NONE', #28697 ) ;
#80929=CARTESIAN_POINT ( 'NONE',  ( 5.292893218813423672, -6.740707523384216415, 5.000000000000000000 ) ) ;
#80930=VECTOR ( 'NONE', #36444, 1000.000000000000114 ) ;
#80931=AXIS2_PLACEMENT_3D ( 'NONE', #46616, #90044, #3038 ) ;
#80932=DIRECTION ( 'NONE',  ( 0.3543493200069162685, -0.000000000000000000, -0.9351131265310288487 ) ) ;
#80933=AXIS2_PLACEMENT_3D ( 'NONE', #73301, #84197, #18146 ) ;
#80934=CARTESIAN_POINT ( 'NONE',  ( 30.48921356237309510, -27.52281430457076894, 5.000000000000000000 ) ) ;
#80935=CARTESIAN_POINT ( 'NONE',  ( -42.48921356237308800, -27.52281430457085065, 5.000000000000000000 ) ) ;
#80936=ADVANCED_FACE ( 'NONE', ( #109071 ), #119928, .F. ) ;
#80937=DIRECTION ( 'NONE',  ( -0.6830127018922181881, 0.6830127018922202975, -0.2588190451025214056 ) ) ;
#80939=AXIS2_PLACEMENT_3D ( 'NONE', #41039, #19286, #63544 ) ;
#80940=FACE_OUTER_BOUND ( 'NONE', #128620, .T. ) ;
#80942=CARTESIAN_POINT ( 'NONE',  ( -1.773258392821650098, -11.24070752338416135, 18.24660765846982358 ) ) ;
#80943=DIRECTION ( 'NONE',  ( -0.000000000000000000, 0.3543493200069153248, 0.9351131265310292928 ) ) ;
#80944=DIRECTION ( 'NONE',  ( 0.7071067811865486830, -0.7071067811865464625, -0.000000000000000000 ) ) ;
#80946=VERTEX_POINT ( 'NONE', #66317 ) ;
#80947=ORIENTED_EDGE ( 'NONE', *, *, #83540, .F. ) ;
#80948=DIRECTION ( 'NONE',  ( 0.7071067811865486830, -0.7071067811865464625, -0.000000000000000000 ) ) ;
#80949=CARTESIAN_POINT ( 'NONE',  ( 14.99451991528749595, 28.92564299267948513, 4.000000000000000000 ) ) ;
#80950=VECTOR ( 'NONE', #91998, 1000.000000000000000 ) ;
#80951=DIRECTION ( 'NONE',  ( -0.7071067811865487940, 0.7071067811865463515, -0.000000000000000000 ) ) ;
#80952=FACE_OUTER_BOUND ( 'NONE', #108650, .T. ) ;
#80953=CARTESIAN_POINT ( 'NONE',  ( 16.49999999999987921, -20.56887692260760758, 4.000000000000000000 ) ) ;
#80955=DIRECTION ( 'NONE',  ( 0.7071067811865487940, -0.7071067811865463515, 0.000000000000000000 ) ) ;
#80956=LINE ( 'NONE', #115667, #52960 ) ;
#80957=CARTESIAN_POINT ( 'NONE',  ( 36.29974487139159578, -27.71228299555231445, 4.000000000000000000 ) ) ;
#80958=CARTESIAN_POINT ( 'NONE',  ( -10.49999999999992184, 3.431123077392145948, 4.000000000000000000 ) ) ;
#80959=CARTESIAN_POINT ( 'NONE',  ( 14.70025512860841133, -27.71228299555195917, 4.000000000000000000 ) ) ;
#80960=FACE_OUTER_BOUND ( 'NONE', #86939, .T. ) ;
#80961=ORIENTED_EDGE ( 'NONE', *, *, #78698, .T. ) ;
#80962=EDGE_CURVE ( 'NONE', #31098, #129128, #140983, .T. ) ;
#80963=VERTEX_POINT ( 'NONE', #9765 ) ;
#80966=ORIENTED_EDGE ( 'NONE', *, *, #80544, .F. ) ;
#80968=CARTESIAN_POINT ( 'NONE',  ( 12.45983838949732281, 18.75929247661552779, 8.305906642995514844 ) ) ;
#80969=EDGE_CURVE ( 'NONE', #74762, #131532, #143142, .T. ) ;
#80970=ORIENTED_EDGE ( 'NONE', *, *, #126098, .T. ) ;
#80971=DIRECTION ( 'NONE',  ( -0.7071067811865486830, -0.7071067811865464625, 0.000000000000000000 ) ) ;
#80972=VERTEX_POINT ( 'NONE', #52560 ) ;
#80973=VERTEX_POINT ( 'NONE', #42438 ) ;
#80974=CARTESIAN_POINT ( 'NONE',  ( -39.29974487139159578, -27.71228299555233576, 4.000000000000000000 ) ) ;
#80977=EDGE_CURVE ( 'NONE', #47233, #30840, #85905, .T. ) ;
#80978=DIRECTION ( 'NONE',  ( 0.7071067811865487940, -0.7071067811865463515, 0.000000000000000000 ) ) ;
#80979=ORIENTED_EDGE ( 'NONE', *, *, #81230, .T. ) ;
#80980=EDGE_CURVE ( 'NONE', #79052, #97544, #130145, .T. ) ;
#80981=PLANE ( 'NONE',  #42358 ) ;
#80983=EDGE_CURVE ( 'NONE', #32103, #76991, #96742, .T. ) ;
#80984=DIRECTION ( 'NONE',  ( -0.7071067811865487940, 0.7071067811865463515, 0.000000000000000000 ) ) ;
#80986=DIRECTION ( 'NONE',  ( -0.7071067811865486830, -0.7071067811865464625, -0.000000000000000000 ) ) ;
#80987=PLANE ( 'NONE',  #111423 ) ;
#80988=LINE ( 'NONE', #91165, #117205 ) ;
#80990=EDGE_LOOP ( 'NONE', ( #21538, #117850, #97936, #67444 ) ) ;
#80991=PLANE ( 'NONE',  #106830 ) ;
#80992=EDGE_CURVE ( 'NONE', #83227, #130423, #97481, .T. ) ;
#80995=DIRECTION ( 'NONE',  ( -0.000000000000000000, -0.3543493200069152693, 0.9351131265310292928 ) ) ;
#80997=VECTOR ( 'NONE', #58269, 1000.000000000000000 ) ;
#80998=LINE ( 'NONE', #127333, #77070 ) ;
#80999=CARTESIAN_POINT ( 'NONE',  ( 31.49999999999978684, -9.462702396500981550, -9.474982329943586024 ) ) ;
#81000=ORIENTED_EDGE ( 'NONE', *, *, #56820, .F. ) ;
#81003=VECTOR ( 'NONE', #141547, 999.9999999999998863 ) ;
#81004=LINE ( 'NONE', #36076, #109056 ) ;
#81005=AXIS2_PLACEMENT_3D ( 'NONE', #81455, #2397, #35814 ) ;
#81006=ADVANCED_FACE ( 'NONE', ( #30841 ), #44594, .F. ) ;
#81007=DIRECTION ( 'NONE',  ( -1.000000000000000000, -1.155222954767600912E-14, 0.000000000000000000 ) ) ;
#81009=ADVANCED_FACE ( 'NONE', ( #41691 ), #30088, .F. ) ;
#81010=FACE_OUTER_BOUND ( 'NONE', #128023, .T. ) ;
#81011=DIRECTION ( 'NONE',  ( -0.000000000000000000, -0.3543493200069152693, 0.9351131265310292928 ) ) ;
#81012=EDGE_LOOP ( 'NONE', ( #115760, #56174, #7946, #53659 ) ) ;
#81013=LINE ( 'NONE', #37511, #4269 ) ;
#81014=LINE ( 'NONE', #125219, #8225 ) ;
#81015=DIRECTION ( 'NONE',  ( -0.7071067811865486830, 0.7071067811865464625, 0.000000000000000000 ) ) ;
#81016=VECTOR ( 'NONE', #128064, 1000.000000000000227 ) ;
#81017=EDGE_CURVE ( 'NONE', #123046, #116750, #8310, .T. ) ;
#81019=ORIENTED_EDGE ( 'NONE', *, *, #97157, .F. ) ;
#81020=EDGE_LOOP ( 'NONE', ( #139945, #73349, #15230, #115299 ) ) ;
#81021=ORIENTED_EDGE ( 'NONE', *, *, #63399, .F. ) ;
#81024=ORIENTED_EDGE ( 'NONE', *, *, #83966, .F. ) ;
#81025=CARTESIAN_POINT ( 'NONE',  ( -23.93182425469048979, -0.2601698552150356059, 4.222180570310114511 ) ) ;
#81027=VECTOR ( 'NONE', #19698, 1000.000000000000000 ) ;
#81028=LINE ( 'NONE', #94008, #138346 ) ;
#81029=CARTESIAN_POINT ( 'NONE',  ( -33.88837638105221117, 9.759292476615614831, 17.35367589129220534 ) ) ;
#81030=ORIENTED_EDGE ( 'NONE', *, *, #76961, .T. ) ;
#81031=DIRECTION ( 'NONE',  ( 1.000000000000000000, 0.000000000000000000, 0.000000000000000000 ) ) ;
#81032=PLANE ( 'NONE',  #109117 ) ;
#81033=AXIS2_PLACEMENT_3D ( 'NONE', #2697, #69423, #25898 ) ;
#81035=ORIENTED_EDGE ( 'NONE', *, *, #33590, .F. ) ;
#81036=DIRECTION ( 'NONE',  ( 0.7071067811865487940, 0.7071067811865463515, -0.000000000000000000 ) ) ;
#81038=LINE ( 'NONE', #132028, #131190 ) ;
#81039=LINE ( 'NONE', #37535, #91004 ) ;
#81040=AXIS2_PLACEMENT_3D ( 'NONE', #75839, #75146, #121459 ) ;
#81042=VERTEX_POINT ( 'NONE', #88057 ) ;
#81044=LINE ( 'NONE', #27334, #127965 ) ;
#81048=CARTESIAN_POINT ( 'NONE',  ( -11.99999999999992006, -0.2811185226894441502, -5.995736974527487106 ) ) ;
#81051=EDGE_CURVE ( 'NONE', #94676, #57817, #10468, .T. ) ;
#81052=DIRECTION ( 'NONE',  ( -0.3543493200069162685, -0.000000000000000000, -0.9351131265310288487 ) ) ;
#81053=LINE ( 'NONE', #49143, #9488 ) ;
#81054=AXIS2_PLACEMENT_3D ( 'NONE', #123517, #24172, #68426 ) ;
#81056=ORIENTED_EDGE ( 'NONE', *, *, #92112, .T. ) ;
#81057=LINE ( 'NONE', #101355, #103532 ) ;
#81058=EDGE_CURVE ( 'NONE', #4187, #97296, #118528, .T. ) ;
#81059=EDGE_LOOP ( 'NONE', ( #3299, #77762, #38606, #109249 ) ) ;
#81060=AXIS2_PLACEMENT_3D ( 'NONE', #47336, #91506, #135717 ) ;
#81061=PLANE ( 'NONE',  #35837 ) ;
#81062=ORIENTED_EDGE ( 'NONE', *, *, #49297, .T. ) ;
#81063=CARTESIAN_POINT ( 'NONE',  ( 2.999999999999985345, 5.966399257802200040, 5.000000000000000000 ) ) ;
#81064=CARTESIAN_POINT ( 'NONE',  ( -53.99451991528749062, 28.92564299267975869, 4.000000000000000000 ) ) ;
#81065=EDGE_CURVE ( 'NONE', #23940, #71937, #294, .T. ) ;
#81066=CARTESIAN_POINT ( 'NONE',  ( 32.53839644629409378, -9.740707523384184441, 17.74957260769618728 ) ) ;
#81067=CARTESIAN_POINT ( 'NONE',  ( -22.49999999999984723, -10.53360074219763121, 5.000000000000000000 ) ) ;
#81068=VECTOR ( 'NONE', #140273, 1000.000000000000000 ) ;
#81069=CARTESIAN_POINT ( 'NONE',  ( 19.49999999999986855, 19.39370406404968605, 1.459788787078156513 ) ) ;
#81070=VERTEX_POINT ( 'NONE', #31537 ) ;
#81071=FACE_OUTER_BOUND ( 'NONE', #73369, .T. ) ;
#81072=LINE ( 'NONE', #94056, #44261 ) ;
#81073=ORIENTED_EDGE ( 'NONE', *, *, #29370, .F. ) ;
#81074=DIRECTION ( 'NONE',  ( 0.7071067811865487940, -0.7071067811865463515, 0.000000000000000000 ) ) ;
#81075=ADVANCED_FACE ( 'NONE', ( #19228 ), #63484, .F. ) ;
#81077=VERTEX_POINT ( 'NONE', #35126 ) ;
#81078=LINE ( 'NONE', #80374, #131511 ) ;
#81079=VERTEX_POINT ( 'NONE', #135159 ) ;
#81080=ORIENTED_EDGE ( 'NONE', *, *, #17745, .F. ) ;
#81081=CARTESIAN_POINT ( 'NONE',  ( -5.292893218813415679, -18.74070752338409562, 5.000000000000000000 ) ) ;
#81083=ORIENTED_EDGE ( 'NONE', *, *, #68943, .F. ) ;
#81085=CARTESIAN_POINT ( 'NONE',  ( -2.576721541936451310, 11.25929247661560240, 17.85071094206585229 ) ) ;
#81087=CARTESIAN_POINT ( 'NONE',  ( 36.18398860626899705, 28.73617430169812437, 5.000000000000000000 ) ) ;
#81088=LINE ( 'NONE', #13646, #99121 ) ;
#81089=LINE ( 'NONE', #80386, #2685 ) ;
#81090=CARTESIAN_POINT ( 'NONE',  ( 15.48921356237309510, -27.52281430457066236, 5.000000000000000000 ) ) ;
#81092=EDGE_CURVE ( 'NONE', #89124, #127280, #56890, .T. ) ;
#81093=DIRECTION ( 'NONE',  ( -0.6830127018922181881, 0.6830127018922202975, -0.2588190451025214056 ) ) ;
#81094=LINE ( 'NONE', #127426, #106133 ) ;
#81095=VECTOR ( 'NONE', #50604, 1000.000000000000227 ) ;
#81096=EDGE_LOOP ( 'NONE', ( #85543, #73587, #78709, #29823 ) ) ;
#81097=EDGE_CURVE ( 'NONE', #139613, #16650, #2437, .T. ) ;
#81098=DIRECTION ( 'NONE',  ( -0.000000000000000000, -0.3543493200069152693, 0.9351131265310292928 ) ) ;
#81099=CARTESIAN_POINT ( 'NONE',  ( 21.29974487139158512, -27.71228299555221142, 4.000000000000000000 ) ) ;
#81100=ORIENTED_EDGE ( 'NONE', *, *, #116592, .F. ) ;
#81101=ORIENTED_EDGE ( 'NONE', *, *, #897, .T. ) ;
#81102=DIRECTION ( 'NONE',  ( 0.7071067811865486830, -0.7071067811865464625, -0.000000000000000000 ) ) ;
#81103=VECTOR ( 'NONE', #98909, 1000.000000000000000 ) ;
#81104=VERTEX_POINT ( 'NONE', #36525 ) ;
#81105=VECTOR ( 'NONE', #94982, 1000.000000000000000 ) ;
#81106=AXIS2_PLACEMENT_3D ( 'NONE', #94776, #30251, #61500 ) ;
#81107=CARTESIAN_POINT ( 'NONE',  ( 27.18398860626900060, 28.73617430169806042, 5.000000000000000000 ) ) ;
#81109=LINE ( 'NONE', #12951, #59537 ) ;
#81110=CARTESIAN_POINT ( 'NONE',  ( 23.53839644629415062, -9.740707523384177335, 17.74957260769616241 ) ) ;
#81112=DIRECTION ( 'NONE',  ( -0.7071067811865487940, 0.7071067811865463515, 0.000000000000000000 ) ) ;
#81113=VERTEX_POINT ( 'NONE', #1706 ) ;
#81115=VECTOR ( 'NONE', #43538, 1000.000000000000000 ) ;
#81116=ORIENTED_EDGE ( 'NONE', *, *, #95198, .F. ) ;
#81117=DIRECTION ( 'NONE',  ( -0.7071067811865487940, 0.7071067811865463515, 0.000000000000000000 ) ) ;
#81119=CARTESIAN_POINT ( 'NONE',  ( 0.3281693992235254487, 2.259292476615687661, 4.000000000000000000 ) ) ;
#81121=ORIENTED_EDGE ( 'NONE', *, *, #55796, .F. ) ;
#81123=ORIENTED_EDGE ( 'NONE', *, *, #65488, .T. ) ;
#81124=CARTESIAN_POINT ( 'NONE',  ( -34.92382263987071411, 21.75929247661549226, 4.252424926123421933 ) ) ;
#81125=VECTOR ( 'NONE', #61542, 1000.000000000000227 ) ;
#81126=LINE ( 'NONE', #5656, #134396 ) ;
#81127=CARTESIAN_POINT ( 'NONE',  ( -7.499999999999944045, -13.53360074219760101, 5.000000000000000000 ) ) ;
#81128=DIRECTION ( 'NONE',  ( -0.7071067811865487940, 0.7071067811865463515, -0.000000000000000000 ) ) ;
#81130=DIRECTION ( 'NONE',  ( 0.7071067811865486830, -0.7071067811865464625, -0.000000000000000000 ) ) ;
#81133=AXIS2_PLACEMENT_3D ( 'NONE', #58832, #102300, #37010 ) ;
#81134=DIRECTION ( 'NONE',  ( 0.6830127018922180770, -0.6830127018922204085, -0.2588190451025213501 ) ) ;
#81135=CARTESIAN_POINT ( 'NONE',  ( 27.32816939922334143, -18.74070752338409562, 4.000000000000000000 ) ) ;
#81136=AXIS2_PLACEMENT_3D ( 'NONE', #56930, #103242, #122866 ) ;
#81137=VERTEX_POINT ( 'NONE', #90179 ) ;
#81139=AXIS2_PLACEMENT_3D ( 'NONE', #85048, #6723, #131422 ) ;
#81140=VERTEX_POINT ( 'NONE', #111206 ) ;
#81141=DIRECTION ( 'NONE',  ( 0.7071067811865487940, -0.7071067811865463515, 0.000000000000000000 ) ) ;
#81142=ORIENTED_EDGE ( 'NONE', *, *, #4742, .F. ) ;
#81143=ORIENTED_EDGE ( 'NONE', *, *, #4833, .T. ) ;
#81146=VERTEX_POINT ( 'NONE', #90931 ) ;
#81148=CARTESIAN_POINT ( 'NONE',  ( 27.70710678118635428, 11.25929247661560062, 5.000000000000000000 ) ) ;
#81149=CARTESIAN_POINT ( 'NONE',  ( 17.99451991528748351, 28.92564299267950645, 4.000000000000000000 ) ) ;
#81152=CARTESIAN_POINT ( 'NONE',  ( -16.49999999999988276, -7.533600742197656963, 5.000000000000000000 ) ) ;
#81153=VECTOR ( 'NONE', #85847, 1000.000000000000000 ) ;
#81154=DIRECTION ( 'NONE',  ( 0.000000000000000000, 0.3543493200069153248, 0.9351131265310291818 ) ) ;
#81157=CARTESIAN_POINT ( 'NONE',  ( 0.000000000000000000, 0.000000000000000000, 5.000000000000000000 ) ) ;
#81159=PLANE ( 'NONE',  #134025 ) ;
#81161=VECTOR ( 'NONE', #129642, 1000.000000000000000 ) ;
#81163=DIRECTION ( 'NONE',  ( 1.000000000000000000, 0.000000000000000000, 0.000000000000000000 ) ) ;
#81164=CARTESIAN_POINT ( 'NONE',  ( -36.48921356237310221, -27.52281430457080802, 5.000000000000000000 ) ) ;
#81165=LINE ( 'NONE', #126092, #96296 ) ;
#81166=EDGE_CURVE ( 'NONE', #36536, #33570, #114082, .T. ) ;
#81167=ORIENTED_EDGE ( 'NONE', *, *, #44381, .F. ) ;
#81168=EDGE_LOOP ( 'NONE', ( #138808, #134354, #88717, #32292 ) ) ;
#81172=CARTESIAN_POINT ( 'NONE',  ( 18.70710678118642178, 17.25929247661554200, 5.000000000000000000 ) ) ;
#81173=CARTESIAN_POINT ( 'NONE',  ( -5.510786437626906675, -27.52281430457051314, 5.000000000000000000 ) ) ;
#81174=VECTOR ( 'NONE', #129039, 1000.000000000000000 ) ;
#81176=ORIENTED_EDGE ( 'NONE', *, *, #22497, .T. ) ;
#81177=LINE ( 'NONE', #25336, #55579 ) ;
#81180=DIRECTION ( 'NONE',  ( 0.6830127018922181881, 0.6830127018922202975, -0.2588190451025214056 ) ) ;
#81182=EDGE_CURVE ( 'NONE', #138807, #17766, #67774, .T. ) ;
#81183=PLANE ( 'NONE',  #7637 ) ;
#81184=FACE_OUTER_BOUND ( 'NONE', #23380, .T. ) ;
#81187=VECTOR ( 'NONE', #93644, 1000.000000000000000 ) ;
#81188=DIRECTION ( 'NONE',  ( 0.3543493200069162685, -0.000000000000000000, -0.9351131265310288487 ) ) ;
#81189=DIRECTION ( 'NONE',  ( 0.6830127018922181881, 0.6830127018922202975, -0.2588190451025214056 ) ) ;
#81191=FACE_OUTER_BOUND ( 'NONE', #45141, .T. ) ;
#81192=EDGE_CURVE ( 'NONE', #131602, #5802, #1017, .T. ) ;
#81193=CARTESIAN_POINT ( 'NONE',  ( 0.000000000000000000, 0.000000000000000000, 5.000000000000000000 ) ) ;
#81194=ORIENTED_EDGE ( 'NONE', *, *, #83500, .F. ) ;
#81195=EDGE_LOOP ( 'NONE', ( #136616, #72, #58793, #76411 ) ) ;
#81198=LINE ( 'NONE', #7136, #112718 ) ;
#81199=EDGE_CURVE ( 'NONE', #119390, #73106, #122822, .T. ) ;
#81200=DIRECTION ( 'NONE',  ( -0.7071067811865487940, 0.7071067811865463515, 0.000000000000000000 ) ) ;
#81201=VERTEX_POINT ( 'NONE', #16157 ) ;
#81202=AXIS2_PLACEMENT_3D ( 'NONE', #15067, #99388, #22539 ) ;
#81203=LINE ( 'NONE', #37701, #102269 ) ;
#81204=CARTESIAN_POINT ( 'NONE',  ( 5.510786437626906675, -27.52281430457051314, 5.000000000000000000 ) ) ;
#81208=ORIENTED_EDGE ( 'NONE', *, *, #86497, .F. ) ;
#81209=VERTEX_POINT ( 'NONE', #82206 ) ;
#81210=CARTESIAN_POINT ( 'NONE',  ( 39.29974487139159578, -27.71228299555233576, 4.000000000000000000 ) ) ;
#81211=ADVANCED_FACE ( 'NONE', ( #94458 ), #105338, .F. ) ;
#81212=AXIS2_PLACEMENT_3D ( 'NONE', #82725, #36364, #3682 ) ;
#81213=AXIS2_PLACEMENT_3D ( 'NONE', #38180, #82396, #115677 ) ;
#81214=CARTESIAN_POINT ( 'NONE',  ( 0.1839886062690032631, 28.73617430169787568, 5.000000000000000000 ) ) ;
#81215=AXIS2_PLACEMENT_3D ( 'NONE', #36028, #27249, #136022 ) ;
#81216=VECTOR ( 'NONE', #139341, 1000.000000000000114 ) ;
#81217=LINE ( 'NONE', #39119, #54744 ) ;
#81218=AXIS2_PLACEMENT_3D ( 'NONE', #72214, #52547, #140970 ) ;
#81220=ORIENTED_EDGE ( 'NONE', *, *, #122546, .F. ) ;
#81221=ORIENTED_EDGE ( 'NONE', *, *, #112792, .F. ) ;
#81223=LINE ( 'NONE', #13766, #46138 ) ;
#81225=EDGE_CURVE ( 'NONE', #47109, #117707, #37241, .T. ) ;
#81226=LINE ( 'NONE', #136287, #91651 ) ;
#81227=ORIENTED_EDGE ( 'NONE', *, *, #23993, .T. ) ;
#81228=ORIENTED_EDGE ( 'NONE', *, *, #138799, .T. ) ;
#81229=DIRECTION ( 'NONE',  ( 1.000000000000000000, 0.000000000000000000, 0.000000000000000000 ) ) ;
#81230=EDGE_CURVE ( 'NONE', #37537, #57989, #50977, .T. ) ;
#81231=VERTEX_POINT ( 'NONE', #92309 ) ;
#81232=ORIENTED_EDGE ( 'NONE', *, *, #55023, .T. ) ;
#81233=AXIS2_PLACEMENT_3D ( 'NONE', #50471, #127296, #70122 ) ;
#81234=CARTESIAN_POINT ( 'NONE',  ( 4.499999999999962697, 1.030536316426508670, -5.498701923753811727 ) ) ;
#81235=AXIS2_PLACEMENT_3D ( 'NONE', #79981, #79277, #102433 ) ;
#81236=AXIS2_PLACEMENT_3D ( 'NONE', #17676, #82272, #7519 ) ;
#81237=CARTESIAN_POINT ( 'NONE',  ( 36.18398860626899705, 28.73617430169812437, 5.000000000000000000 ) ) ;
#81238=VERTEX_POINT ( 'NONE', #137277 ) ;
#81239=LINE ( 'NONE', #34877, #27465 ) ;
#81240=ADVANCED_FACE ( 'NONE', ( #71311 ), #29206, .F. ) ;
#81241=VECTOR ( 'NONE', #38550, 999.9999999999998863 ) ;
#81242=FACE_OUTER_BOUND ( 'NONE', #87608, .T. ) ;
#81243=VECTOR ( 'NONE', #129089, 1000.000000000000000 ) ;
#81245=CARTESIAN_POINT ( 'NONE',  ( 10.99806943317893726, -22.22500000000000142, 4.500000000000000888 ) ) ;
#81246=FACE_BOUND ( 'NONE', #58836, .T. ) ;
#81248=DIRECTION ( 'NONE',  ( 0.6830127018922180770, -0.6830127018922204085, -0.2588190451025213501 ) ) ;
#81249=CARTESIAN_POINT ( 'NONE',  ( -5.999999999999963585, -16.06887692260763956, 4.000000000000000000 ) ) ;
#81250=EDGE_CURVE ( 'NONE', #65792, #128178, #73449, .T. ) ;
#81252=EDGE_LOOP ( 'NONE', ( #49601, #53980, #52752, #130881 ) ) ;
#81254=ORIENTED_EDGE ( 'NONE', *, *, #6792, .F. ) ;
#81255=ORIENTED_EDGE ( 'NONE', *, *, #97767, .F. ) ;
#81256=ORIENTED_EDGE ( 'NONE', *, *, #87459, .T. ) ;
#81258=ORIENTED_EDGE ( 'NONE', *, *, #67133, .T. ) ;
#81259=AXIS2_PLACEMENT_3D ( 'NONE', #48155, #61224, #105368 ) ;
#81261=CARTESIAN_POINT ( 'NONE',  ( 39.18398860626899705, 28.73617430169814568, 5.000000000000000000 ) ) ;
#81263=CARTESIAN_POINT ( 'NONE',  ( -7.499999999999940492, 1.087461875839228931, 4.000000000000000000 ) ) ;
#81264=VERTEX_POINT ( 'NONE', #82901 ) ;
#81266=VECTOR ( 'NONE', #9255, 1000.000000000000227 ) ;
#81268=DIRECTION ( 'NONE',  ( -0.7071067811865486830, 0.7071067811865464625, 0.000000000000000000 ) ) ;
#81269=PLANE ( 'NONE',  #131957 ) ;
#81270=ADVANCED_FACE ( 'NONE', ( #26373 ), #70627, .F. ) ;
#81271=DIRECTION ( 'NONE',  ( 0.7071067811865486830, -0.7071067811865464625, -0.000000000000000000 ) ) ;
#81272=CARTESIAN_POINT ( 'NONE',  ( 57.29974487139158157, -27.71228299555246011, 4.000000000000000000 ) ) ;
#81273=ORIENTED_EDGE ( 'NONE', *, *, #52701, .T. ) ;
#81274=ORIENTED_EDGE ( 'NONE', *, *, #115544, .T. ) ;
#81275=ORIENTED_EDGE ( 'NONE', *, *, #121246, .T. ) ;
#81277=EDGE_LOOP ( 'NONE', ( #40187, #15527, #39323, #139154 ) ) ;
#81279=ORIENTED_EDGE ( 'NONE', *, *, #69015, .F. ) ;
#81280=VERTEX_POINT ( 'NONE', #136532 ) ;
#81281=DIRECTION ( 'NONE',  ( 0.6830127018922181881, 0.6830127018922202975, -0.2588190451025214056 ) ) ;
#81282=FACE_OUTER_BOUND ( 'NONE', #18646, .T. ) ;
#81284=EDGE_CURVE ( 'NONE', #103836, #126734, #104629, .T. ) ;
#81285=CARTESIAN_POINT ( 'NONE',  ( -27.29974487139158512, -27.71228299555225405, 4.000000000000000000 ) ) ;
#81286=ORIENTED_EDGE ( 'NONE', *, *, #31726, .F. ) ;
#81287=CARTESIAN_POINT ( 'NONE',  ( 12.48921356237309155, -27.52281430457064104, 5.000000000000000000 ) ) ;
#81288=VECTOR ( 'NONE', #132375, 1000.000000000000000 ) ;
#81290=CARTESIAN_POINT ( 'NONE',  ( -15.70701326429294475, -21.74070752338406365, 4.999753212805219782 ) ) ;
#81291=CARTESIAN_POINT ( 'NONE',  ( 42.48921356237308800, -27.52281430457085065, 5.000000000000000000 ) ) ;
#81293=EDGE_LOOP ( 'NONE', ( #27423, #50771, #61709, #66115 ) ) ;
#81295=DIRECTION ( 'NONE',  ( -0.3543493200069162685, -0.000000000000000000, -0.9351131265310288487 ) ) ;
#81297=ORIENTED_EDGE ( 'NONE', *, *, #109828, .T. ) ;
#81298=ORIENTED_EDGE ( 'NONE', *, *, #12222, .F. ) ;
#81299=DIRECTION ( 'NONE',  ( -0.7071067811865486830, -0.7071067811865464625, 0.000000000000000000 ) ) ;
#81300=VERTEX_POINT ( 'NONE', #116226 ) ;
#81301=DIRECTION ( 'NONE',  ( -0.7071067811865487940, 0.7071067811865463515, 0.000000000000000000 ) ) ;
#81302=LINE ( 'NONE', #47285, #21918 ) ;
#81303=VECTOR ( 'NONE', #6509, 1000.000000000000000 ) ;
#81304=DIRECTION ( 'NONE',  ( -0.3543493200069162685, -0.000000000000000000, -0.9351131265310288487 ) ) ;
#81305=ADVANCED_FACE ( 'NONE', ( #49578 ), #84345, .T. ) ;
#81306=ORIENTED_EDGE ( 'NONE', *, *, #75026, .F. ) ;
#81307=AXIS2_PLACEMENT_3D ( 'NONE', #23649, #100510, #57025 ) ;
#81308=CARTESIAN_POINT ( 'NONE',  ( 45.48921356237309510, -27.52281430457087197, 5.000000000000000000 ) ) ;
#81309=VECTOR ( 'NONE', #92595, 1000.000000000000000 ) ;
#81310=LINE ( 'NONE', #71144, #37204 ) ;
#81313=DIRECTION ( 'NONE',  ( 1.000000000000000000, 0.000000000000000000, 0.000000000000000000 ) ) ;
#81315=VECTOR ( 'NONE', #78650, 1000.000000000000000 ) ;
#81316=VECTOR ( 'NONE', #7995, 999.9999999999998863 ) ;
#81317=VECTOR ( 'NONE', #5730, 999.9999999999998863 ) ;
#81318=LINE ( 'NONE', #115295, #63207 ) ;
#81319=VECTOR ( 'NONE', #78425, 1000.000000000000000 ) ;
#81320=ORIENTED_EDGE ( 'NONE', *, *, #83233, .F. ) ;
#81321=LINE ( 'NONE', #35694, #62576 ) ;
#81322=ORIENTED_EDGE ( 'NONE', *, *, #43583, .F. ) ;
#81323=ORIENTED_EDGE ( 'NONE', *, *, #6430, .F. ) ;
#81325=VECTOR ( 'NONE', #75995, 999.9999999999998863 ) ;
#81326=ORIENTED_EDGE ( 'NONE', *, *, #116340, .T. ) ;
#81327=DIRECTION ( 'NONE',  ( 0.7071067811865486830, -0.7071067811865464625, -0.000000000000000000 ) ) ;
#81329=EDGE_CURVE ( 'NONE', #36068, #60957, #127088, .T. ) ;
#81331=ORIENTED_EDGE ( 'NONE', *, *, #65099, .T. ) ;
#81332=VECTOR ( 'NONE', #106149, 1000.000000000000000 ) ;
#81333=CARTESIAN_POINT ( 'NONE',  ( 45.18398860626900415, 28.73617430169818832, 5.000000000000000000 ) ) ;
#81334=EDGE_CURVE ( 'NONE', #130580, #22223, #16916, .T. ) ;
#81335=CARTESIAN_POINT ( 'NONE',  ( -17.99451991528748351, 28.92564299267950645, 4.000000000000000000 ) ) ;
#81336=DIRECTION ( 'NONE',  ( -0.7071067811865486830, -0.7071067811865464625, 0.000000000000000000 ) ) ;
#81337=CARTESIAN_POINT ( 'NONE',  ( 12.18398860626900060, 28.73617430169795739, 5.000000000000000000 ) ) ;
#81338=CARTESIAN_POINT ( 'NONE',  ( 15.32816939922340005, -21.74070752338407786, 4.000000000000000000 ) ) ;
#81340=PLANE ( 'NONE',  #44193 ) ;
#81341=CARTESIAN_POINT ( 'NONE',  ( 2.999999999999983569, 1.931123077392163712, 4.000000000000000000 ) ) ;
#81342=EDGE_CURVE ( 'NONE', #120324, #3555, #138711, .T. ) ;
#81343=ORIENTED_EDGE ( 'NONE', *, *, #90288, .T. ) ;
#81344=ADVANCED_FACE ( 'NONE', ( #15440 ), #127838, .F. ) ;
#81345=VERTEX_POINT ( 'NONE', #72779 ) ;
#81346=VERTEX_POINT ( 'NONE', #61870 ) ;
#81348=VECTOR ( 'NONE', #72500, 1000.000000000000000 ) ;
#81349=ORIENTED_EDGE ( 'NONE', *, *, #141591, .T. ) ;
#81351=VECTOR ( 'NONE', #7020, 999.9999999999998863 ) ;
#81352=ORIENTED_EDGE ( 'NONE', *, *, #81411, .T. ) ;
#81353=DIRECTION ( 'NONE',  ( 0.7071067811865487940, -0.7071067811865463515, 0.000000000000000000 ) ) ;
#81354=LINE ( 'NONE', #71908, #18459 ) ;
#81355=AXIS2_PLACEMENT_3D ( 'NONE', #8525, #107163, #85401 ) ;
#81356=ORIENTED_EDGE ( 'NONE', *, *, #78589, .F. ) ;
#81357=DIRECTION ( 'NONE',  ( -0.7071067811865487940, 0.7071067811865463515, -0.000000000000000000 ) ) ;
#81358=CARTESIAN_POINT ( 'NONE',  ( -30.79289321881324071, 0.7592924766157069794, 5.000000000000000000 ) ) ;
#81359=ADVANCED_FACE ( 'NONE', ( #40131 ), #117613, .F. ) ;
#81360=LINE ( 'NONE', #125566, #32645 ) ;
#81363=ORIENTED_EDGE ( 'NONE', *, *, #44045, .F. ) ;
#81364=EDGE_CURVE ( 'NONE', #80915, #12285, #68143, .T. ) ;
#81365=FACE_OUTER_BOUND ( 'NONE', #28452, .T. ) ;
#81366=DIRECTION ( 'NONE',  ( -0.7071067811865486830, -0.7071067811865464625, 0.000000000000000000 ) ) ;
#81367=DIRECTION ( 'NONE',  ( 0.7071067811865486830, -0.7071067811865464625, -0.000000000000000000 ) ) ;
#81369=DIRECTION ( 'NONE',  ( -0.6830127018922180770, -0.6830127018922204085, -0.2588190451025213501 ) ) ;
#81370=CARTESIAN_POINT ( 'NONE',  ( -45.48921356237309510, -27.52281430457087197, 5.000000000000000000 ) ) ;
#81371=PLANE ( 'NONE',  #124547 ) ;
#81373=CARTESIAN_POINT ( 'NONE',  ( -24.18398860626899705, 28.73617430169804265, 5.000000000000000000 ) ) ;
#81375=VECTOR ( 'NONE', #40164, 1000.000000000000000 ) ;
#81377=ORIENTED_EDGE ( 'NONE', *, *, #133673, .F. ) ;
#81379=EDGE_CURVE ( 'NONE', #42327, #13174, #134071, .T. ) ;
#81380=VERTEX_POINT ( 'NONE', #89142 ) ;
#81381=ORIENTED_EDGE ( 'NONE', *, *, #87283, .T. ) ;
#81382=DIRECTION ( 'NONE',  ( -0.7071067811865487940, 0.7071067811865463515, -0.000000000000000000 ) ) ;
#81385=DIRECTION ( 'NONE',  ( -0.7071067811865487940, 0.7071067811865463515, -0.000000000000000000 ) ) ;
#81386=ORIENTED_EDGE ( 'NONE', *, *, #52322, .F. ) ;
#81387=EDGE_CURVE ( 'NONE', #19726, #16488, #1372, .T. ) ;
#81388=VECTOR ( 'NONE', #95199, 999.9999999999998863 ) ;
#81390=CARTESIAN_POINT ( 'NONE',  ( -20.67183060077632106, -21.74070752338406010, 4.000000000000000000 ) ) ;
#81391=PLANE ( 'NONE',  #4817 ) ;
#81393=VERTEX_POINT ( 'NONE', #99255 ) ;
#81394=CARTESIAN_POINT ( 'NONE',  ( 13.49999999999990763, -17.56887692260763245, 4.000000000000000000 ) ) ;
#81395=EDGE_LOOP ( 'NONE', ( #94910, #109518, #71565, #80073 ) ) ;
#81396=EDGE_CURVE ( 'NONE', #139855, #31203, #122450, .T. ) ;
#81397=VECTOR ( 'NONE', #141751, 1000.000000000000000 ) ;
#81398=CARTESIAN_POINT ( 'NONE',  ( -32.99999999999976552, 20.96639925780205260, 5.000000000000000000 ) ) ;
#81401=( BOUNDED_CURVE ( )  B_SPLINE_CURVE ( 3, ( #133786, #14124, #67106, #123649 ),
 .UNSPECIFIED., .F., .T. ) 
 B_SPLINE_CURVE_WITH_KNOTS ( ( 4, 4 ),
 ( 3.334020839929784152, 3.401188224464155141 ),
 .UNSPECIFIED. ) 
 CURVE ( )  GEOMETRIC_REPRESENTATION_ITEM ( )  RATIONAL_B_SPLINE_CURVE ( ( 1.000000000000000000, 0.9996240805387412998, 0.9996240805387412998, 1.000000000000000000 ) ) 
 REPRESENTATION_ITEM ( '' )  );
#81402=CARTESIAN_POINT ( 'NONE',  ( -57.48921356237308800, -27.52281430457095368, 5.000000000000000000 ) ) ;
#81403=ORIENTED_EDGE ( 'NONE', *, *, #118797, .T. ) ;
#81404=ORIENTED_EDGE ( 'NONE', *, *, #91168, .T. ) ;
#81405=LINE ( 'NONE', #70546, #42507 ) ;
#81406=PLANE ( 'NONE',  #83305 ) ;
#81408=ADVANCED_FACE ( 'NONE', ( #674 ), #66674, .F. ) ;
#81410=VECTOR ( 'NONE', #104696, 999.9999999999998863 ) ;
#81411=EDGE_CURVE ( 'NONE', #72508, #135668, #17192, .T. ) ;
#81413=LINE ( 'NONE', #69827, #92862 ) ;
#81415=ORIENTED_EDGE ( 'NONE', *, *, #54641, .T. ) ;
#81416=ORIENTED_EDGE ( 'NONE', *, *, #126909, .T. ) ;
#81417=DIRECTION ( 'NONE',  ( -0.7071067811865486830, -0.7071067811865464625, 0.000000000000000000 ) ) ;
#81418=VECTOR ( 'NONE', #123745, 1000.000000000000000 ) ;
#81419=ORIENTED_EDGE ( 'NONE', *, *, #1089, .F. ) ;
#81421=VECTOR ( 'NONE', #101168, 1000.000000000000000 ) ;
#81425=AXIS2_PLACEMENT_3D ( 'NONE', #79573, #123758, #51905 ) ;
#81426=AXIS2_PLACEMENT_3D ( 'NONE', #135716, #33572, #124118 ) ;
#81428=VECTOR ( 'NONE', #112178, 1000.000000000000000 ) ;
#81429=VECTOR ( 'NONE', #27325, 1000.000000000000114 ) ;
#81431=CARTESIAN_POINT ( 'NONE',  ( 18.48921356237309510, -27.52281430457068367, 5.000000000000000000 ) ) ;
#81432=FACE_BOUND ( 'NONE', #35343, .T. ) ;
#81434=CARTESIAN_POINT ( 'NONE',  ( -11.20666063542143753, 21.75929247661549937, 4.998822639870708073 ) ) ;
#81435=VECTOR ( 'NONE', #48923, 1000.000000000000000 ) ;
#81436=CARTESIAN_POINT ( 'NONE',  ( 3.758600742197928835, 21.72499999999999432, 5.000000000000000000 ) ) ;
#81437=VERTEX_POINT ( 'NONE', #33365 ) ;
#81438=CARTESIAN_POINT ( 'NONE',  ( -26.99999999999981171, 7.588810512006185505, -3.013526669885166154 ) ) ;
#81440=ORIENTED_EDGE ( 'NONE', *, *, #79435, .F. ) ;
#81443=AXIS2_PLACEMENT_3D ( 'NONE', #55393, #141684, #42384 ) ;
#81444=CARTESIAN_POINT ( 'NONE',  ( -31.25154412867556175, -11.24070752338416490, 10.39518518046016560 ) ) ;
#81445=DIRECTION ( 'NONE',  ( 0.7071067811865486830, -0.7071067811865464625, -0.000000000000000000 ) ) ;
#81446=VERTEX_POINT ( 'NONE', #40813 ) ;
#81447=CARTESIAN_POINT ( 'NONE',  ( -6.707106781186501721, 5.259292476615663681, 5.000000000000000000 ) ) ;
#81448=AXIS2_PLACEMENT_3D ( 'NONE', #62343, #127581, #60950 ) ;
#81449=VECTOR ( 'NONE', #5398, 1000.000000000000000 ) ;
#81451=LINE ( 'NONE', #82864, #124636 ) ;
#81452=PLANE ( 'NONE',  #31954 ) ;
#81453=VECTOR ( 'NONE', #109598, 1000.000000000000000 ) ;
#81454=PLANE ( 'NONE',  #30795 ) ;
#81455=CARTESIAN_POINT ( 'NONE',  ( 3.183988606268992161, 28.73617430169789699, 5.000000000000000000 ) ) ;
#81456=ORIENTED_EDGE ( 'NONE', *, *, #34489, .F. ) ;
#81457=EDGE_LOOP ( 'NONE', ( #136206, #69364, #62523, #35691 ) ) ;
#81458=VECTOR ( 'NONE', #3736, 999.9999999999998863 ) ;
#81459=LINE ( 'NONE', #114741, #3335 ) ;
#81460=LINE ( 'NONE', #39370, #95240 ) ;
#81461=ORIENTED_EDGE ( 'NONE', *, *, #118073, .F. ) ;
#81462=VERTEX_POINT ( 'NONE', #51700 ) ;
#81463=ORIENTED_EDGE ( 'NONE', *, *, #71392, .F. ) ;
#81464=ADVANCED_FACE ( 'NONE', ( #43486 ), #85016, .F. ) ;
#81465=ADVANCED_FACE ( 'NONE', ( #56557 ), #131933, .F. ) ;
#81466=CARTESIAN_POINT ( 'NONE',  ( 16.49999999999988987, -14.70932175296475819, -11.46312253303840833 ) ) ;
#81467=VERTEX_POINT ( 'NONE', #45657 ) ;
#81468=CARTESIAN_POINT ( 'NONE',  ( -9.183988606268997046, 28.73617430169793607, 5.000000000000000000 ) ) ;
#81469=VECTOR ( 'NONE', #105451, 999.9999999999998863 ) ;
#81470=CARTESIAN_POINT ( 'NONE',  ( 21.18398860626899349, 28.73617430169802134, 5.000000000000000000 ) ) ;
#81472=LINE ( 'NONE', #5276, #77366 ) ;
#81473=VERTEX_POINT ( 'NONE', #107483 ) ;
#81474=EDGE_CURVE ( 'NONE', #14862, #43234, #132675, .T. ) ;
#81475=CARTESIAN_POINT ( 'NONE',  ( -45.18398860626900415, 28.73617430169818832, 5.000000000000000000 ) ) ;
#81477=CARTESIAN_POINT ( 'NONE',  ( 18.29974487139159223, -27.71228299555219010, 4.000000000000000000 ) ) ;
#81478=FACE_OUTER_BOUND ( 'NONE', #75866, .T. ) ;
#81479=ORIENTED_EDGE ( 'NONE', *, *, #141537, .F. ) ;
#81480=CARTESIAN_POINT ( 'NONE',  ( -9.005480084712511157, 28.92564299267931816, 4.000000000000000000 ) ) ;
#81482=ORIENTED_EDGE ( 'NONE', *, *, #138401, .T. ) ;
#81483=CARTESIAN_POINT ( 'NONE',  ( 34.92499999999998295, -21.72500000000000142, 5.000000000000000000 ) ) ;
#81484=CARTESIAN_POINT ( 'NONE',  ( 2.602085213965210642E-15, -15.41253812416060143, 4.000000000000000000 ) ) ;
#81487=ORIENTED_EDGE ( 'NONE', *, *, #67925, .T. ) ;
#81488=CARTESIAN_POINT ( 'NONE',  ( 34.92499999999998295, -12.03857301832750970, 17.98374865626353625 ) ) ;
#81490=DIRECTION ( 'NONE',  ( 0.6830127018922181881, 0.6830127018922202975, -0.2588190451025214056 ) ) ;
#81491=DIRECTION ( 'NONE',  ( 0.7071067811865486830, -0.7071067811865464625, -0.000000000000000000 ) ) ;
#81492=VECTOR ( 'NONE', #106029, 1000.000000000000000 ) ;
#81493=VERTEX_POINT ( 'NONE', #34759 ) ;
#81494=EDGE_CURVE ( 'NONE', #6816, #107486, #140809, .T. ) ;
#81495=DIRECTION ( 'NONE',  ( -0.7071067811865486830, -0.7071067811865464625, 0.000000000000000000 ) ) ;
#81496=LINE ( 'NONE', #79374, #93319 ) ;
#81498=CARTESIAN_POINT ( 'NONE',  ( 10.21321903303352840, 12.75929247661559351, 10.29404684609037623 ) ) ;
#81500=ORIENTED_EDGE ( 'NONE', *, *, #110741, .T. ) ;
#81501=ORIENTED_EDGE ( 'NONE', *, *, #95227, .T. ) ;
#81502=ADVANCED_FACE ( 'NONE', ( #121733 ), #52385, .F. ) ;
#81503=VECTOR ( 'NONE', #79770, 1000.000000000000000 ) ;
#81504=FACE_OUTER_BOUND ( 'NONE', #38621, .T. ) ;
#81506=DIRECTION ( 'NONE',  ( -0.3543493200069162685, -0.000000000000000000, -0.9351131265310288487 ) ) ;
#81507=CARTESIAN_POINT ( 'NONE',  ( 14.16170612452611444, -6.740707523384212863, 16.75550250614870862 ) ) ;
#81508=CARTESIAN_POINT ( 'NONE',  ( -34.92500000000001137, 21.72500000000000142, 5.000000000000000000 ) ) ;
#81509=LINE ( 'NONE', #14790, #97722 ) ;
#81510=ORIENTED_EDGE ( 'NONE', *, *, #137954, .F. ) ;
#81513=DIRECTION ( 'NONE',  ( 0.7071067811865487940, 0.7071067811865463515, -0.000000000000000000 ) ) ;
#81514=VECTOR ( 'NONE', #19737, 1000.000000000000227 ) ;
#81515=PLANE ( 'NONE',  #1825 ) ;
#81518=ADVANCED_FACE ( 'NONE', ( #121032 ), #55084, .T. ) ;
#81519=AXIS2_PLACEMENT_3D ( 'NONE', #34191, #108853, #53818 ) ;
#81520=EDGE_CURVE ( 'NONE', #47269, #90697, #80417, .T. ) ;
#81521=AXIS2_PLACEMENT_3D ( 'NONE', #53789, #107425, #9509 ) ;
#81523=LINE ( 'NONE', #116259, #99750 ) ;
#81525=CARTESIAN_POINT ( 'NONE',  ( -63.48921356237309510, -27.52281430457099631, 5.000000000000000000 ) ) ;
#81526=ORIENTED_EDGE ( 'NONE', *, *, #20737, .T. ) ;
#81527=AXIS2_PLACEMENT_3D ( 'NONE', #13380, #113420, #35193 ) ;
#81528=VECTOR ( 'NONE', #59941, 1000.000000000000000 ) ;
#81529=CARTESIAN_POINT ( 'NONE',  ( -4.499999999999964473, -10.91253812416064761, 4.000000000000000000 ) ) ;
#81531=CARTESIAN_POINT ( 'NONE',  ( -24.29974487139158867, -27.71228299555223273, 4.000000000000000000 ) ) ;
#81532=DIRECTION ( 'NONE',  ( -0.7071067811865486830, -0.7071067811865464625, 0.000000000000000000 ) ) ;
#81533=PLANE ( 'NONE',  #101939 ) ;
#81534=EDGE_CURVE ( 'NONE', #140963, #139479, #113732, .T. ) ;
#81535=FACE_OUTER_BOUND ( 'NONE', #142649, .T. ) ;
#81537=VERTEX_POINT ( 'NONE', #114438 ) ;
#81538=ADVANCED_FACE ( 'NONE', ( #126724 ), #124607, .F. ) ;
#81539=PLANE ( 'NONE',  #120393 ) ;
#81540=DIRECTION ( 'NONE',  ( -0.6830127018922181881, 0.6830127018922202975, -0.2588190451025214056 ) ) ;
#81541=PLANE ( 'NONE',  #139995 ) ;
#81546=ORIENTED_EDGE ( 'NONE', *, *, #12582, .T. ) ;
#81548=EDGE_CURVE ( 'NONE', #108392, #86264, #27412, .T. ) ;
#81549=PLANE ( 'NONE',  #111774 ) ;
#81550=DIRECTION ( 'NONE',  ( -0.6830127018922181881, 0.6830127018922202975, -0.2588190451025214056 ) ) ;
#81551=CARTESIAN_POINT ( 'NONE',  ( 13.08316395874281568, 3.014287036135060660, 4.000000000000000000 ) ) ;
#81552=ORIENTED_EDGE ( 'NONE', *, *, #72208, .F. ) ;
#81554=VECTOR ( 'NONE', #47062, 1000.000000000000000 ) ;
#81555=PLANE ( 'NONE',  #81527 ) ;
#81557=DIRECTION ( 'NONE',  ( 0.7071067811865486830, -0.7071067811865464625, -0.000000000000000000 ) ) ;
#81559=CARTESIAN_POINT ( 'NONE',  ( -24.48921356237309510, -27.52281430457072631, 5.000000000000000000 ) ) ;
#81560=VERTEX_POINT ( 'NONE', #113004 ) ;
#81561=VERTEX_POINT ( 'NONE', #4181 ) ;
#81562=VECTOR ( 'NONE', #82415, 1000.000000000000000 ) ;
#81563=DIRECTION ( 'NONE',  ( 0.7071067811865487940, 0.7071067811865463515, -0.000000000000000000 ) ) ;
#81564=LINE ( 'NONE', #125768, #19742 ) ;
#81565=CARTESIAN_POINT ( 'NONE',  ( -36.29974487139159578, -27.71228299555231445, 4.000000000000000000 ) ) ;
#81566=CARTESIAN_POINT ( 'NONE',  ( 63.18398860626900415, 28.73617430169831621, 5.000000000000000000 ) ) ;
#81567=DIRECTION ( 'NONE',  ( -0.7071067811865487940, 0.7071067811865463515, 0.000000000000000000 ) ) ;
#81568=CARTESIAN_POINT ( 'NONE',  ( 41.99451991528749062, 28.92564299267967343, 4.000000000000000000 ) ) ;
#81570=LINE ( 'NONE', #60535, #11330 ) ;
#81571=LINE ( 'NONE', #125775, #103332 ) ;
#81574=EDGE_CURVE ( 'NONE', #73921, #97839, #57247, .T. ) ;
#81575=ORIENTED_EDGE ( 'NONE', *, *, #61691, .F. ) ;
#81577=ORIENTED_EDGE ( 'NONE', *, *, #25871, .F. ) ;
#81578=CARTESIAN_POINT ( 'NONE',  ( 20.81601139373100295, 28.73617430169773002, 5.000000000000000000 ) ) ;
#81579=DIRECTION ( 'NONE',  ( -0.3543493200069162685, -0.000000000000000000, -0.9351131265310288487 ) ) ;
#81581=CARTESIAN_POINT ( 'NONE',  ( -18.18398860626898994, 28.73617430169800002, 5.000000000000000000 ) ) ;
#81582=CARTESIAN_POINT ( 'NONE',  ( 15.32816939922342314, -12.74070752338415247, 4.000000000000000000 ) ) ;
#81583=EDGE_LOOP ( 'NONE', ( #23311, #46287, #55636, #126854 ) ) ;
#81584=ORIENTED_EDGE ( 'NONE', *, *, #167, .F. ) ;
#81585=VECTOR ( 'NONE', #33395, 1000.000000000000000 ) ;
#81586=FACE_OUTER_BOUND ( 'NONE', #15208, .T. ) ;
#81587=CARTESIAN_POINT ( 'NONE',  ( 78.48921356237309510, -27.52281430457109934, 5.000000000000000000 ) ) ;
#81588=ORIENTED_EDGE ( 'NONE', *, *, #104586, .F. ) ;
#81589=VERTEX_POINT ( 'NONE', #2071 ) ;
#81590=FACE_OUTER_BOUND ( 'NONE', #124480, .T. ) ;
#81591=DIRECTION ( 'NONE',  ( -0.7071067811865487940, 0.7071067811865463515, -0.000000000000000000 ) ) ;
#81592=VECTOR ( 'NONE', #15986, 1000.000000000000000 ) ;
#81593=FACE_BOUND ( 'NONE', #108099, .T. ) ;
#81594=DIRECTION ( 'NONE',  ( -0.7071067811865486830, -0.7071067811865464625, 0.000000000000000000 ) ) ;
#81596=DIRECTION ( 'NONE',  ( -0.000000000000000000, 0.000000000000000000, 1.000000000000000000 ) ) ;
#81597=VECTOR ( 'NONE', #11770, 1000.000000000000000 ) ;
#81598=CARTESIAN_POINT ( 'NONE',  ( -23.20710678118638981, 15.75929247661555976, 5.000000000000000000 ) ) ;
#81599=DIRECTION ( 'NONE',  ( -0.000000000000000000, 0.000000000000000000, 1.000000000000000000 ) ) ;
#81602=ORIENTED_EDGE ( 'NONE', *, *, #25966, .F. ) ;
#81604=VERTEX_POINT ( 'NONE', #70283 ) ;
#81605=CARTESIAN_POINT ( 'NONE',  ( -13.17183060077637613, -14.24070752338413648, 4.000000000000000000 ) ) ;
#81607=CARTESIAN_POINT ( 'NONE',  ( 72.48921356237309510, -27.52281430457106026, 5.000000000000000000 ) ) ;
#81608=VECTOR ( 'NONE', #52757, 1000.000000000000000 ) ;
#81611=FACE_OUTER_BOUND ( 'NONE', #124766, .T. ) ;
#81612=VECTOR ( 'NONE', #70622, 1000.000000000000227 ) ;
#81614=FACE_OUTER_BOUND ( 'NONE', #37096, .T. ) ;
#81615=ORIENTED_EDGE ( 'NONE', *, *, #49271, .T. ) ;
#81617=CARTESIAN_POINT ( 'NONE',  ( 16.77149322861325231, 20.25929247661551713, 7.808871592221806601 ) ) ;
#81618=CARTESIAN_POINT ( 'NONE',  ( 20.52487387214941350, 14.25929247661557042, 9.797011795316684868 ) ) ;
#81619=CARTESIAN_POINT ( 'NONE',  ( -15.67180000000000284, 3.174999999999997158, 1.444000000000000394 ) ) ;
#81620=LINE ( 'NONE', #48980, #93671 ) ;
#81622=VECTOR ( 'NONE', #141622, 1000.000000000000000 ) ;
#81625=DIRECTION ( 'NONE',  ( 0.6830127018922181881, 0.6830127018922202975, -0.2588190451025214056 ) ) ;
#81626=ORIENTED_EDGE ( 'NONE', *, *, #125066, .T. ) ;
#81627=DIRECTION ( 'NONE',  ( 0.7071067811865487940, -0.7071067811865463515, 0.000000000000000000 ) ) ;
#81628=CARTESIAN_POINT ( 'NONE',  ( 17.99451991528748351, 28.92564299267950645, 4.000000000000000000 ) ) ;
#81629=EDGE_CURVE ( 'NONE', #142812, #25609, #13673, .T. ) ;
#81631=ORIENTED_EDGE ( 'NONE', *, *, #115661, .T. ) ;
#81632=ADVANCED_FACE ( 'NONE', ( #104252 ), #92671, .F. ) ;
#81633=EDGE_CURVE ( 'NONE', #68934, #58171, #134804, .T. ) ;
#81634=ORIENTED_EDGE ( 'NONE', *, *, #136201, .F. ) ;
#81636=ORIENTED_EDGE ( 'NONE', *, *, #96015, .F. ) ;
#81638=EDGE_CURVE ( 'NONE', #42005, #42538, #91973, .T. ) ;
#81641=ORIENTED_EDGE ( 'NONE', *, *, #135880, .T. ) ;
#81642=EDGE_CURVE ( 'NONE', #77572, #68590, #129604, .T. ) ;
#81643=DIRECTION ( 'NONE',  ( 0.6830127018922180770, -0.6830127018922204085, -0.2588190451025213501 ) ) ;
#81644=ORIENTED_EDGE ( 'NONE', *, *, #97203, .T. ) ;
#81645=CARTESIAN_POINT ( 'NONE',  ( 34.42499999999998295, 22.22500000000000142, 4.165035510187007795 ) ) ;
#81646=DIRECTION ( 'NONE',  ( -0.7071067811865486830, 0.7071067811865464625, 0.000000000000000000 ) ) ;
#81648=ORIENTED_EDGE ( 'NONE', *, *, #142856, .T. ) ;
#81649=ORIENTED_EDGE ( 'NONE', *, *, #68274, .F. ) ;
#81650=FACE_OUTER_BOUND ( 'NONE', #71717, .T. ) ;
#81651=VECTOR ( 'NONE', #115597, 1000.000000000000000 ) ;
#81652=DIRECTION ( 'NONE',  ( -0.7071067811865486830, -0.7071067811865464625, 0.000000000000000000 ) ) ;
#81656=ORIENTED_EDGE ( 'NONE', *, *, #66006, .F. ) ;
#81657=EDGE_LOOP ( 'NONE', ( #45632, #110859, #138944, #42842 ) ) ;
#81658=AXIS2_PLACEMENT_3D ( 'NONE', #88961, #109967, #133179 ) ;
#81659=ORIENTED_EDGE ( 'NONE', *, *, #137980, .T. ) ;
#81661=DIRECTION ( 'NONE',  ( 0.6830127018922181881, 0.6830127018922202975, -0.2588190451025214056 ) ) ;
#81662=VECTOR ( 'NONE', #37321, 1000.000000000000000 ) ;
#81663=VECTOR ( 'NONE', #52275, 1000.000000000000000 ) ;
#81665=CARTESIAN_POINT ( 'NONE',  ( 24.48921356237309510, -27.52281430457072631, 5.000000000000000000 ) ) ;
#81666=FACE_OUTER_BOUND ( 'NONE', #9495, .T. ) ;
#81667=DIRECTION ( 'NONE',  ( -0.000000000000000000, -0.3543493200069152693, 0.9351131265310292928 ) ) ;
#81668=CARTESIAN_POINT ( 'NONE',  ( 0.000000000000000000, 0.000000000000000000, 5.000000000000000000 ) ) ;
#81669=ORIENTED_EDGE ( 'NONE', *, *, #96381, .T. ) ;
#81670=EDGE_CURVE ( 'NONE', #117172, #42180, #128195, .T. ) ;
#81671=DIRECTION ( 'NONE',  ( 0.7071067811865486830, -0.7071067811865464625, -0.000000000000000000 ) ) ;
#81674=LINE ( 'NONE', #6890, #80797 ) ;
#81675=CARTESIAN_POINT ( 'NONE',  ( -18.18398860626898994, 28.73617430169800002, 5.000000000000000000 ) ) ;
#81677=VERTEX_POINT ( 'NONE', #106378 ) ;
#81679=ADVANCED_FACE ( 'NONE', ( #41891 ), #96227, .F. ) ;
#81680=ORIENTED_EDGE ( 'NONE', *, *, #98511, .F. ) ;
#81681=PLANE ( 'NONE',  #34888 ) ;
#81682=DIRECTION ( 'NONE',  ( -0.7071067811865486830, -0.7071067811865464625, -0.000000000000000000 ) ) ;
#81683=LINE ( 'NONE', #114274, #103211 ) ;
#81685=CARTESIAN_POINT ( 'NONE',  ( -32.20710678118632586, 6.759292476615653023, 5.000000000000000000 ) ) ;
#81689=EDGE_CURVE ( 'NONE', #119254, #23935, #138344, .T. ) ;
#81691=DIRECTION ( 'NONE',  ( -0.7071067811865487940, 0.7071067811865463515, 0.000000000000000000 ) ) ;
#81692=DIRECTION ( 'NONE',  ( 0.7071067811865487940, 0.7071067811865463515, 0.000000000000000000 ) ) ;
#81693=EDGE_CURVE ( 'NONE', #47322, #85488, #104986, .T. ) ;
#81694=DIRECTION ( 'NONE',  ( 0.7071067811865486830, -0.7071067811865464625, -0.000000000000000000 ) ) ;
#81695=ORIENTED_EDGE ( 'NONE', *, *, #9444, .F. ) ;
#81696=VECTOR ( 'NONE', #38944, 999.9999999999998863 ) ;
#81698=ORIENTED_EDGE ( 'NONE', *, *, #129720, .T. ) ;
#81699=EDGE_CURVE ( 'NONE', #70901, #41454, #61532, .T. ) ;
#81700=CARTESIAN_POINT ( 'NONE',  ( -8.700255128608413102, -27.71228299555199825, 4.000000000000000000 ) ) ;
#81701=CARTESIAN_POINT ( 'NONE',  ( -14.59243874171183641, 22.22500000000000142, 12.70476753181831775 ) ) ;
#81703=DIRECTION ( 'NONE',  ( -0.000000000000000000, 0.3543493200069153248, 0.9351131265310292928 ) ) ;
#81705=VERTEX_POINT ( 'NONE', #49924 ) ;
#81706=CARTESIAN_POINT ( 'NONE',  ( -33.79289321881321939, -17.24070752338409918, 5.000000000000000000 ) ) ;
#81708=ORIENTED_EDGE ( 'NONE', *, *, #38996, .F. ) ;
#81710=ORIENTED_EDGE ( 'NONE', *, *, #92274, .T. ) ;
#81713=PLANE ( 'NONE',  #69531 ) ;
#81715=ORIENTED_EDGE ( 'NONE', *, *, #65780, .T. ) ;
#81716=EDGE_CURVE ( 'NONE', #27773, #21069, #73109, .T. ) ;
#81717=DIRECTION ( 'NONE',  ( 0.6830127018922181881, 0.6830127018922202975, -0.2588190451025214056 ) ) ;
#81718=DIRECTION ( 'NONE',  ( 0.6830127018922181881, 0.6830127018922202975, -0.2588190451025214056 ) ) ;
#81722=VECTOR ( 'NONE', #111028, 1000.000000000000000 ) ;
#81723=DIRECTION ( 'NONE',  ( 0.7071067811865486830, -0.7071067811865464625, -0.000000000000000000 ) ) ;
#81724=ORIENTED_EDGE ( 'NONE', *, *, #119414, .F. ) ;
#81726=VECTOR ( 'NONE', #57411, 999.9999999999998863 ) ;
#81727=AXIS2_PLACEMENT_3D ( 'NONE', #62006, #129363, #93181 ) ;
#81728=CARTESIAN_POINT ( 'NONE',  ( -0.4892135623730947680, -27.52281430457055578, 5.000000000000000000 ) ) ;
#81729=VERTEX_POINT ( 'NONE', #83249 ) ;
#81730=EDGE_CURVE ( 'NONE', #60519, #79079, #130334, .T. ) ;
#81732=DIRECTION ( 'NONE',  ( -0.7071067811865486830, -0.7071067811865464625, 0.000000000000000000 ) ) ;
#81733=VECTOR ( 'NONE', #104980, 999.9999999999998863 ) ;
#81734=CARTESIAN_POINT ( 'NONE',  ( -6.707106781186484845, -18.74070752338408852, 5.000000000000000000 ) ) ;
#81737=FACE_OUTER_BOUND ( 'NONE', #2886, .T. ) ;
#81739=CARTESIAN_POINT ( 'NONE',  ( 23.51078643762690490, -27.52281430457038880, 5.000000000000000000 ) ) ;
#81740=DIRECTION ( 'NONE',  ( -0.7071067811865487940, -0.7071067811865463515, -0.000000000000000000 ) ) ;
#81741=ORIENTED_EDGE ( 'NONE', *, *, #34820, .F. ) ;
#81742=CARTESIAN_POINT ( 'NONE',  ( 0.000000000000000000, 0.000000000000000000, 5.000000000000000000 ) ) ;
#81743=DIRECTION ( 'NONE',  ( 0.7071067811865487940, -0.7071067811865463515, 0.000000000000000000 ) ) ;
#81744=CARTESIAN_POINT ( 'NONE',  ( -34.49999999999976552, -1.535744391599501490, 4.994342998332164996 ) ) ;
#81746=CARTESIAN_POINT ( 'NONE',  ( -6.183988606268994381, 28.73617430169791476, 5.000000000000000000 ) ) ;
#81750=EDGE_LOOP ( 'NONE', ( #122394, #43522, #117580, #123585 ) ) ;
#81752=VERTEX_POINT ( 'NONE', #95532 ) ;
#81753=ORIENTED_EDGE ( 'NONE', *, *, #137694, .T. ) ;
#81755=AXIS2_PLACEMENT_3D ( 'NONE', #85929, #42464, #117809 ) ;
#81756=ORIENTED_EDGE ( 'NONE', *, *, #6442, .T. ) ;
#81757=EDGE_CURVE ( 'NONE', #129447, #28284, #72415, .T. ) ;
#81758=CARTESIAN_POINT ( 'NONE',  ( 33.18398860626899705, 28.73617430169810305, 5.000000000000000000 ) ) ;
#81759=CARTESIAN_POINT ( 'NONE',  ( 6.299744871391586898, -27.71228299555210484, 4.000000000000000000 ) ) ;
#81760=CARTESIAN_POINT ( 'NONE',  ( -24.34427593291135139, 5.931737808750704666, 4.000000000000000000 ) ) ;
#81761=FACE_OUTER_BOUND ( 'NONE', #45557, .T. ) ;
#81762=ORIENTED_EDGE ( 'NONE', *, *, #51388, .F. ) ;
#81763=CARTESIAN_POINT ( 'NONE',  ( 15.72281430457048934, -21.72500000000000497, 5.000000000000000000 ) ) ;
#81764=DIRECTION ( 'NONE',  ( -0.000000000000000000, 0.3543493200069153248, 0.9351131265310292928 ) ) ;
#81765=VECTOR ( 'NONE', #5623, 1000.000000000000000 ) ;
#81768=VERTEX_POINT ( 'NONE', #118714 ) ;
#81769=VECTOR ( 'NONE', #61354, 1000.000000000000000 ) ;
#81770=CARTESIAN_POINT ( 'NONE',  ( 15.79076468313838433, 8.175634574663693144, 5.000000000000000000 ) ) ;
#81771=CARTESIAN_POINT ( 'NONE',  ( 54.29974487139159578, -27.71228299555243879, 4.000000000000000000 ) ) ;
#81772=CARTESIAN_POINT ( 'NONE',  ( -3.330102185472624932, 17.25929247661554555, 19.83885114516072079 ) ) ;
#81773=ORIENTED_EDGE ( 'NONE', *, *, #39223, .T. ) ;
#81774=EDGE_LOOP ( 'NONE', ( #141954, #87747, #110336, #101008 ) ) ;
#81775=LINE ( 'NONE', #91891, #28410 ) ;
#81776=EDGE_CURVE ( 'NONE', #139533, #30840, #107823, .T. ) ;
#81778=DIRECTION ( 'NONE',  ( -0.6830127018922181881, 0.6830127018922202975, -0.2588190451025214056 ) ) ;
#81779=CARTESIAN_POINT ( 'NONE',  ( 8.999999999999950262, 2.587461875839218273, 4.000000000000000000 ) ) ;
#81781=CARTESIAN_POINT ( 'NONE',  ( -1.499999999999990896, 15.43112307739202471, 4.000000000000000000 ) ) ;
#81782=AXIS2_PLACEMENT_3D ( 'NONE', #38341, #14446, #104277 ) ;
#81783=DIRECTION ( 'NONE',  ( 0.3543493200069163240, -0.000000000000000000, 0.9351131265310288487 ) ) ;
#81784=VERTEX_POINT ( 'NONE', #116584 ) ;
#81785=ORIENTED_EDGE ( 'NONE', *, *, #132696, .F. ) ;
#81786=DIRECTION ( 'NONE',  ( -0.7071067811865487940, 0.7071067811865463515, 0.000000000000000000 ) ) ;
#81787=ORIENTED_EDGE ( 'NONE', *, *, #9186, .F. ) ;
#81788=VECTOR ( 'NONE', #71429, 1000.000000000000000 ) ;
#81789=AXIS2_PLACEMENT_3D ( 'NONE', #6396, #103602, #28217 ) ;
#81791=LINE ( 'NONE', #83933, #12705 ) ;
#81792=VERTEX_POINT ( 'NONE', #50618 ) ;
#81794=DIRECTION ( 'NONE',  ( 0.7071067811865487940, 0.7071067811865463515, 0.000000000000000000 ) ) ;
#81795=LINE ( 'NONE', #57903, #25297 ) ;
#81796=VECTOR ( 'NONE', #90782, 1000.000000000000000 ) ;
#81797=LINE ( 'NONE', #36136, #141660 ) ;
#81798=ORIENTED_EDGE ( 'NONE', *, *, #91138, .T. ) ;
#81799=EDGE_CURVE ( 'NONE', #132568, #99900, #28873, .T. ) ;
#81800=DIRECTION ( 'NONE',  ( 0.6830127018922181881, 0.6830127018922202975, -0.2588190451025214056 ) ) ;
#81802=ORIENTED_EDGE ( 'NONE', *, *, #55586, .F. ) ;
#81803=CARTESIAN_POINT ( 'NONE',  ( 23.99451991528749062, 28.92564299267954908, 4.000000000000000000 ) ) ;
#81804=VERTEX_POINT ( 'NONE', #128879 ) ;
#81805=EDGE_CURVE ( 'NONE', #76331, #116521, #29559, .T. ) ;
#81806=ORIENTED_EDGE ( 'NONE', *, *, #125858, .F. ) ;
#81807=ADVANCED_FACE ( 'NONE', ( #117968 ), #62948, .T. ) ;
#81808=DIRECTION ( 'NONE',  ( -0.6830127018922180770, -0.6830127018922204085, -0.2588190451025213501 ) ) ;
#81809=ORIENTED_EDGE ( 'NONE', *, *, #26144, .T. ) ;
#81810=ORIENTED_EDGE ( 'NONE', *, *, #83350, .T. ) ;
#81811=VECTOR ( 'NONE', #128615, 1000.000000000000000 ) ;
#81813=VERTEX_POINT ( 'NONE', #66504 ) ;
#81814=EDGE_CURVE ( 'NONE', #2927, #47322, #88977, .T. ) ;
#81817=DIRECTION ( 'NONE',  ( 0.6830127018922180770, -0.6830127018922204085, -0.2588190451025213501 ) ) ;
#81820=DIRECTION ( 'NONE',  ( -0.7071067811865487940, 0.7071067811865463515, -0.000000000000000000 ) ) ;
#81821=ADVANCED_FACE ( 'NONE', ( #99827 ), #493, .F. ) ;
#81822=LINE ( 'NONE', #112977, #136195 ) ;
#81823=CARTESIAN_POINT ( 'NONE',  ( -34.92382263987071411, 21.75929247661549226, 4.252424926123421933 ) ) ;
#81824=CARTESIAN_POINT ( 'NONE',  ( 6.183988606268994381, 28.73617430169791476, 5.000000000000000000 ) ) ;
#81825=VECTOR ( 'NONE', #64533, 1000.000000000000000 ) ;
#81826=ADVANCED_FACE ( 'NONE', ( #87530 ), #122270, .F. ) ;
#81828=VECTOR ( 'NONE', #137787, 1000.000000000000000 ) ;
#81829=LINE ( 'NONE', #82509, #100021 ) ;
#81832=VERTEX_POINT ( 'NONE', #31721 ) ;
#81833=CARTESIAN_POINT ( 'NONE',  ( -29.99999999999979039, -21.03360074219752462, 5.000000000000000000 ) ) ;
#81834=DIRECTION ( 'NONE',  ( -0.3543493200069162685, -0.000000000000000000, -0.9351131265310288487 ) ) ;
#81835=VERTEX_POINT ( 'NONE', #20105 ) ;
#81836=EDGE_LOOP ( 'NONE', ( #140807, #85609, #30945, #57419 ) ) ;
#81837=AXIS2_PLACEMENT_3D ( 'NONE', #101687, #47376, #79986 ) ;
#81838=ORIENTED_EDGE ( 'NONE', *, *, #69380, .T. ) ;
#81840=ORIENTED_EDGE ( 'NONE', *, *, #134164, .F. ) ;
#81841=CARTESIAN_POINT ( 'NONE',  ( 24.34427593291135139, 5.931737808750704666, 4.000000000000000000 ) ) ;
#81842=CARTESIAN_POINT ( 'NONE',  ( -19.49999999999985434, 13.08746187583910725, 4.000000000000000000 ) ) ;
#81843=EDGE_CURVE ( 'NONE', #73190, #22203, #132503, .T. ) ;
#81844=FACE_OUTER_BOUND ( 'NONE', #124517, .T. ) ;
#81845=FACE_OUTER_BOUND ( 'NONE', #137182, .T. ) ;
#81846=EDGE_LOOP ( 'NONE', ( #105826, #83525, #4605, #13411, #132671, #29851 ) ) ;
#81847=CARTESIAN_POINT ( 'NONE',  ( 27.79289321881326558, 3.759292476615680112, 5.000000000000000000 ) ) ;
#81848=EDGE_LOOP ( 'NONE', ( #8980, #100139, #143072, #99939 ) ) ;
#81853=PLANE ( 'NONE',  #82965 ) ;
#81854=PLANE ( 'NONE',  #7249 ) ;
#81855=ORIENTED_EDGE ( 'NONE', *, *, #138477, .F. ) ;
#81856=ORIENTED_EDGE ( 'NONE', *, *, #89250, .F. ) ;
#81857=ORIENTED_EDGE ( 'NONE', *, *, #62378, .F. ) ;
#81858=CARTESIAN_POINT ( 'NONE',  ( -69.48921356237309510, -27.52281430457103895, 5.000000000000000000 ) ) ;
#81859=DIRECTION ( 'NONE',  ( 0.7071067811865487940, 0.7071067811865463515, 0.000000000000000000 ) ) ;
#81860=CARTESIAN_POINT ( 'NONE',  ( 0.000000000000000000, 0.000000000000000000, 5.000000000000000000 ) ) ;
#81863=AXIS2_PLACEMENT_3D ( 'NONE', #18462, #51864, #126532 ) ;
#81864=DIRECTION ( 'NONE',  ( -0.6830127018922180770, -0.6830127018922204085, -0.2588190451025213501 ) ) ;
#81866=CARTESIAN_POINT ( 'NONE',  ( -21.98911971346036154, -22.02621442084248216, 4.990779571109221990 ) ) ;
#81867=AXIS2_PLACEMENT_3D ( 'NONE', #126155, #26822, #58074 ) ;
#81868=FACE_OUTER_BOUND ( 'NONE', #44077, .T. ) ;
#81869=CARTESIAN_POINT ( 'NONE',  ( -34.92500000000001137, 21.72500000000000142, 5.000000000000000000 ) ) ;
#81871=VERTEX_POINT ( 'NONE', #46201 ) ;
#81873=CARTESIAN_POINT ( 'NONE',  ( 0.1839886062690032631, 28.73617430169787568, 5.000000000000000000 ) ) ;
#81874=ORIENTED_EDGE ( 'NONE', *, *, #55110, .T. ) ;
#81875=EDGE_CURVE ( 'NONE', #96656, #114250, #36027, .T. ) ;
#81876=AXIS2_PLACEMENT_3D ( 'NONE', #98913, #22067, #87352 ) ;
#81877=DIRECTION ( 'NONE',  ( -0.6830127018922180770, -0.6830127018922204085, -0.2588190451025213501 ) ) ;
#81880=CARTESIAN_POINT ( 'NONE',  ( -2.816011393730999401, 28.73617430169785436, 5.000000000000000000 ) ) ;
#81881=LINE ( 'NONE', #49241, #95605 ) ;
#81882=CARTESIAN_POINT ( 'NONE',  ( -15.48921356237309510, -27.52281430457066236, 5.000000000000000000 ) ) ;
#81883=ORIENTED_EDGE ( 'NONE', *, *, #32017, .T. ) ;
#81885=ORIENTED_EDGE ( 'NONE', *, *, #92325, .T. ) ;
#81887=VECTOR ( 'NONE', #101909, 999.9999999999998863 ) ;
#81888=DIRECTION ( 'NONE',  ( -0.3543493200069162685, -0.000000000000000000, -0.9351131265310288487 ) ) ;
#81889=FACE_OUTER_BOUND ( 'NONE', #36395, .T. ) ;
#81891=PLANE ( 'NONE',  #92453 ) ;
#81894=ADVANCED_FACE ( 'NONE', ( #15623 ), #81681, .F. ) ;
#81895=DIRECTION ( 'NONE',  ( -0.7071067811865486830, -0.7071067811865464625, -0.000000000000000000 ) ) ;
#81897=FACE_OUTER_BOUND ( 'NONE', #25578, .T. ) ;
#81900=VECTOR ( 'NONE', #75301, 1000.000000000000000 ) ;
#81901=CARTESIAN_POINT ( 'NONE',  ( -21.87889065874226091, 8.431076354171498366, 5.000000000000000000 ) ) ;
#81903=DIRECTION ( 'NONE',  ( 1.000000000000000000, 0.000000000000000000, 0.000000000000000000 ) ) ;
#81904=VERTEX_POINT ( 'NONE', #112152 ) ;
#81905=ORIENTED_EDGE ( 'NONE', *, *, #66494, .F. ) ;
#81907=ORIENTED_EDGE ( 'NONE', *, *, #14377, .F. ) ;
#81908=VERTEX_POINT ( 'NONE', #57072 ) ;
#81909=EDGE_CURVE ( 'NONE', #17986, #69434, #90376, .T. ) ;
#81910=CARTESIAN_POINT ( 'NONE',  ( -14.70025512860841133, -27.71228299555195917, 4.000000000000000000 ) ) ;
#81912=VECTOR ( 'NONE', #78607, 1000.000000000000000 ) ;
#81913=DIRECTION ( 'NONE',  ( -0.3543493200069162685, -0.000000000000000000, -0.9351131265310288487 ) ) ;
#81914=EDGE_LOOP ( 'NONE', ( #133002, #53583, #38582, #48916 ) ) ;
#81916=FACE_OUTER_BOUND ( 'NONE', #34026, .T. ) ;
#81919=ADVANCED_FACE ( 'NONE', ( #103372 ), #92500, .T. ) ;
#81920=EDGE_CURVE ( 'NONE', #8586, #100840, #37442, .T. ) ;
#81921=CARTESIAN_POINT ( 'NONE',  ( -33.18398860626899705, 28.73617430169810305, 5.000000000000000000 ) ) ;
#81924=PLANE ( 'NONE',  #132802 ) ;
#81925=FACE_OUTER_BOUND ( 'NONE', #135318, .T. ) ;
#81928=LINE ( 'NONE', #39096, #8227 ) ;
#81929=CARTESIAN_POINT ( 'NONE',  ( -26.99999999999980105, -16.44781430457065241, 5.000000000000000000 ) ) ;
#81931=ORIENTED_EDGE ( 'NONE', *, *, #77495, .F. ) ;
#81932=ORIENTED_EDGE ( 'NONE', *, *, #111719, .F. ) ;
#81936=FACE_OUTER_BOUND ( 'NONE', #113014, .T. ) ;
#81939=DIRECTION ( 'NONE',  ( -0.000000000000000000, 0.000000000000000000, 1.000000000000000000 ) ) ;
#81940=PLANE ( 'NONE',  #7155 ) ;
#81941=AXIS2_PLACEMENT_3D ( 'NONE', #66612, #71606, #127391 ) ;
#81942=EDGE_CURVE ( 'NONE', #136439, #141981, #130489, .T. ) ;
#81944=EDGE_CURVE ( 'NONE', #1174, #140583, #113542, .T. ) ;
#81946=ORIENTED_EDGE ( 'NONE', *, *, #34651, .T. ) ;
#81947=DIRECTION ( 'NONE',  ( 0.7071067811865487940, 0.7071067811865463515, 0.000000000000000000 ) ) ;
#81948=PLANE ( 'NONE',  #56473 ) ;
#81949=DIRECTION ( 'NONE',  ( -0.6830127018922180770, -0.6830127018922204085, -0.2588190451025213501 ) ) ;
#81950=ORIENTED_EDGE ( 'NONE', *, *, #104313, .F. ) ;
#81951=ORIENTED_EDGE ( 'NONE', *, *, #123510, .T. ) ;
#81952=VERTEX_POINT ( 'NONE', #59224 ) ;
#81953=LINE ( 'NONE', #5016, #70041 ) ;
#81954=EDGE_CURVE ( 'NONE', #110220, #124632, #72253, .T. ) ;
#81958=LINE ( 'NONE', #137013, #22189 ) ;
#81960=ORIENTED_EDGE ( 'NONE', *, *, #57198, .T. ) ;
#81961=LINE ( 'NONE', #90676, #50191 ) ;
#81962=ORIENTED_EDGE ( 'NONE', *, *, #2146, .F. ) ;
#81963=ORIENTED_EDGE ( 'NONE', *, *, #127275, .F. ) ;
#81964=DIRECTION ( 'NONE',  ( -0.6830127018922180770, -0.6830127018922204085, -0.2588190451025213501 ) ) ;
#81965=LINE ( 'NONE', #20206, #2633 ) ;
#81967=VECTOR ( 'NONE', #117450, 1000.000000000000000 ) ;
#81968=CARTESIAN_POINT ( 'NONE',  ( 41.99451991528749062, 28.92564299267967343, 4.000000000000000000 ) ) ;
#81969=LINE ( 'NONE', #50031, #108469 ) ;
#81970=CARTESIAN_POINT ( 'NONE',  ( -39.48921356237310221, -27.52281430457082934, 5.000000000000000000 ) ) ;
#81971=VECTOR ( 'NONE', #140823, 1000.000000000000000 ) ;
#81972=CARTESIAN_POINT ( 'NONE',  ( 5.999999999999952927, -3.412538124160716002, 4.000000000000000000 ) ) ;
#81973=FACE_BOUND ( 'NONE', #32553, .T. ) ;
#81975=ORIENTED_EDGE ( 'NONE', *, *, #102796, .T. ) ;
#81976=CARTESIAN_POINT ( 'NONE',  ( 33.70710678118631165, -12.74070752338415247, 5.000000000000000000 ) ) ;
#81977=CARTESIAN_POINT ( 'NONE',  ( -11.70025512860841133, -27.71228299555198049, 4.000000000000000000 ) ) ;
#81979=VERTEX_POINT ( 'NONE', #82379 ) ;
#81980=CYLINDRICAL_SURFACE ( 'NONE', #32053, 3.378199999999994319 ) ;
#81981=ORIENTED_EDGE ( 'NONE', *, *, #132387, .F. ) ;
#81983=( BOUNDED_CURVE ( )  B_SPLINE_CURVE ( 3, ( #119427, #128894, #20121, #108537 ),
 .UNSPECIFIED., .F., .T. ) 
 B_SPLINE_CURVE_WITH_KNOTS ( ( 4, 4 ),
 ( 5.106027341939297415, 6.645403452391243526 ),
 .UNSPECIFIED. ) 
 CURVE ( )  GEOMETRIC_REPRESENTATION_ITEM ( )  RATIONAL_B_SPLINE_CURVE ( ( 1.000000000000000000, 0.8120851936182322817, 0.8120851936182322817, 1.000000000000000000 ) ) 
 REPRESENTATION_ITEM ( '' )  );
#81984=ORIENTED_EDGE ( 'NONE', *, *, #110116, .F. ) ;
#81986=ADVANCED_FACE ( 'NONE', ( #51896 ), #96076, .F. ) ;
#81988=VECTOR ( 'NONE', #80395, 1000.000000000000000 ) ;
#81989=ORIENTED_EDGE ( 'NONE', *, *, #59524, .F. ) ;
#81990=DIRECTION ( 'NONE',  ( -0.3543493200069162685, -0.000000000000000000, -0.9351131265310288487 ) ) ;
#81991=EDGE_CURVE ( 'NONE', #645, #79854, #30110, .T. ) ;
#81992=FACE_OUTER_BOUND ( 'NONE', #60933, .T. ) ;
#81993=CARTESIAN_POINT ( 'NONE',  ( -24.48921356237309510, -27.52281430457072631, 5.000000000000000000 ) ) ;
#81994=EDGE_LOOP ( 'NONE', ( #55164, #47331, #74868, #33245 ) ) ;
#81995=EDGE_CURVE ( 'NONE', #115605, #96412, #83082, .T. ) ;
#81996=CARTESIAN_POINT ( 'NONE',  ( -17.20710678118641468, -14.24070752338413648, 5.000000000000000000 ) ) ;
#81997=CARTESIAN_POINT ( 'NONE',  ( -8.671830600776413434, 2.259292476615694323, 4.000000000000000000 ) ) ;
#81998=VECTOR ( 'NONE', #99851, 1000.000000000000000 ) ;
#81999=EDGE_CURVE ( 'NONE', #68379, #56807, #138903, .T. ) ;
#82001=CARTESIAN_POINT ( 'NONE',  ( 34.92499999999998295, 22.22500000000000142, 4.000000000000000000 ) ) ;
#82002=DIRECTION ( 'NONE',  ( -0.7071067811865486830, -0.7071067811865464625, -0.000000000000000000 ) ) ;
#82003=CARTESIAN_POINT ( 'NONE',  ( 21.48921356237309155, -27.52281430457070499, 5.000000000000000000 ) ) ;
#82004=LINE ( 'NONE', #116728, #107232 ) ;
#82005=ADVANCED_FACE ( 'NONE', ( #128721 ), #139638, .T. ) ;
#82008=ORIENTED_EDGE ( 'NONE', *, *, #135412, .F. ) ;
#82009=ORIENTED_EDGE ( 'NONE', *, *, #9571, .F. ) ;
#82011=ORIENTED_EDGE ( 'NONE', *, *, #70924, .T. ) ;
#82014=EDGE_CURVE ( 'NONE', #100660, #101323, #41001, .T. ) ;
#82015=EDGE_CURVE ( 'NONE', #132444, #93212, #17789, .T. ) ;
#82016=DIRECTION ( 'NONE',  ( 0.3543493200069162685, -0.000000000000000000, -0.9351131265310288487 ) ) ;
#82017=ORIENTED_EDGE ( 'NONE', *, *, #82678, .F. ) ;
#82019=ORIENTED_EDGE ( 'NONE', *, *, #18970, .F. ) ;
#82020=ADVANCED_FACE ( 'NONE', ( #93943 ), #38861, .T. ) ;
#82021=DIRECTION ( 'NONE',  ( 0.3543493200069162685, -0.000000000000000000, -0.9351131265310288487 ) ) ;
#82022=DIRECTION ( 'NONE',  ( 0.7071067811865487940, 0.7071067811865463515, 0.000000000000000000 ) ) ;
#82023=VECTOR ( 'NONE', #44200, 999.9999999999998863 ) ;
#82025=ORIENTED_EDGE ( 'NONE', *, *, #6359, .F. ) ;
#82027=LINE ( 'NONE', #126888, #133298 ) ;
#82029=EDGE_LOOP ( 'NONE', ( #104778, #63702, #47616, #62566 ) ) ;
#82030=FACE_OUTER_BOUND ( 'NONE', #52233, .T. ) ;
#82032=LINE ( 'NONE', #82717, #39485 ) ;
#82034=CARTESIAN_POINT ( 'NONE',  ( -72.18398860626899705, 28.73617430169837661, 5.000000000000000000 ) ) ;
#82035=LINE ( 'NONE', #37056, #49329 ) ;
#82037=AXIS2_PLACEMENT_3D ( 'NONE', #71996, #84978, #6652 ) ;
#82038=EDGE_LOOP ( 'NONE', ( #71375, #137184, #137803, #116170 ) ) ;
#82039=LINE ( 'NONE', #71865, #124653 ) ;
#82040=DIRECTION ( 'NONE',  ( -0.7071067811865486830, -0.7071067811865464625, -0.000000000000000000 ) ) ;
#82042=EDGE_CURVE ( 'NONE', #41011, #71142, #94644, .T. ) ;
#82043=ORIENTED_EDGE ( 'NONE', *, *, #28965, .T. ) ;
#82044=CARTESIAN_POINT ( 'NONE',  ( -32.67183060077623935, 11.25929247661560240, 4.000000000000000000 ) ) ;
#82045=LINE ( 'NONE', #113918, #636 ) ;
#82046=EDGE_LOOP ( 'NONE', ( #130767, #60333, #130233, #43987 ) ) ;
#82047=DIRECTION ( 'NONE',  ( -0.7071067811865486830, 0.7071067811865464625, 0.000000000000000000 ) ) ;
#82049=ORIENTED_EDGE ( 'NONE', *, *, #14990, .F. ) ;
#82050=CARTESIAN_POINT ( 'NONE',  ( 34.49999999999975842, -11.94567065516892512, 4.994342998332160555 ) ) ;
#82051=CARTESIAN_POINT ( 'NONE',  ( 0.06011071044020009635, -9.740707523384184441, 10.89222023123380900 ) ) ;
#82052=VECTOR ( 'NONE', #63615, 999.9999999999998863 ) ;
#82053=VERTEX_POINT ( 'NONE', #104822 ) ;
#82054=LINE ( 'NONE', #126237, #39613 ) ;
#82056=CARTESIAN_POINT ( 'NONE',  ( -31.49999999999977973, 21.05218569542895679, 5.000000000000000000 ) ) ;
#82057=VECTOR ( 'NONE', #55662, 1000.000000000000000 ) ;
#82058=DIRECTION ( 'NONE',  ( -0.000000000000000000, 0.3543493200069153248, 0.9351131265310292928 ) ) ;
#82059=ORIENTED_EDGE ( 'NONE', *, *, #140904, .F. ) ;
#82060=CARTESIAN_POINT ( 'NONE',  ( 8.865004262483717312, 3.759292476615678336, 15.36553568819724269 ) ) ;
#82061=VECTOR ( 'NONE', #53321, 1000.000000000000000 ) ;
#82062=DIRECTION ( 'NONE',  ( -0.7071067811865486830, -0.7071067811865464625, 0.000000000000000000 ) ) ;
#82063=EDGE_CURVE ( 'NONE', #115378, #20512, #137468, .T. ) ;
#82065=LINE ( 'NONE', #60299, #56409 ) ;
#82066=FACE_OUTER_BOUND ( 'NONE', #97097, .T. ) ;
#82067=DIRECTION ( 'NONE',  ( 0.7071067811865486830, -0.7071067811865464625, -0.000000000000000000 ) ) ;
#82069=DIRECTION ( 'NONE',  ( -0.3543493200069162685, -0.000000000000000000, -0.9351131265310288487 ) ) ;
#82070=ORIENTED_EDGE ( 'NONE', *, *, #74778, .T. ) ;
#82071=ORIENTED_EDGE ( 'NONE', *, *, #15378, .F. ) ;
#82074=VERTEX_POINT ( 'NONE', #8330 ) ;
#82075=AXIS2_PLACEMENT_3D ( 'NONE', #88979, #34585, #33192 ) ;
#82076=ORIENTED_EDGE ( 'NONE', *, *, #6492, .T. ) ;
#82077=EDGE_CURVE ( 'NONE', #120532, #20063, #106221, .T. ) ;
#82078=ORIENTED_EDGE ( 'NONE', *, *, #103114, .F. ) ;
#82079=DIRECTION ( 'NONE',  ( -0.7071067811865486830, -0.7071067811865464625, -0.000000000000000000 ) ) ;
#82080=CARTESIAN_POINT ( 'NONE',  ( -31.49999999999977973, -10.91253812416064584, 4.000000000000000000 ) ) ;
#82082=LINE ( 'NONE', #105902, #32393 ) ;
#82083=DIRECTION ( 'NONE',  ( 0.3543493200069162685, -0.000000000000000000, -0.9351131265310288487 ) ) ;
#82084=VECTOR ( 'NONE', #48292, 1000.000000000000227 ) ;
#82085=CARTESIAN_POINT ( 'NONE',  ( 20.67183060077632106, -3.740707523384244837, 4.000000000000000000 ) ) ;
#82087=ADVANCED_FACE ( 'NONE', ( #6895 ), #52580, .F. ) ;
#82088=VERTEX_POINT ( 'NONE', #84527 ) ;
#82090=PLANE ( 'NONE',  #35375 ) ;
#82091=LINE ( 'NONE', #59611, #116681 ) ;
#82092=DIRECTION ( 'NONE',  ( -0.6830127018922181881, 0.6830127018922202975, -0.2588190451025214056 ) ) ;
#82093=DIRECTION ( 'NONE',  ( -0.6830127018922180770, -0.6830127018922204085, -0.2588190451025213501 ) ) ;
#82094=VECTOR ( 'NONE', #40633, 1000.000000000000000 ) ;
#82096=FACE_OUTER_BOUND ( 'NONE', #17041, .T. ) ;
#82099=ORIENTED_EDGE ( 'NONE', *, *, #26051, .T. ) ;
#82100=VERTEX_POINT ( 'NONE', #19248 ) ;
#82101=VECTOR ( 'NONE', #66678, 1000.000000000000000 ) ;
#82103=ORIENTED_EDGE ( 'NONE', *, *, #109906, .T. ) ;
#82104=ORIENTED_EDGE ( 'NONE', *, *, #21754, .F. ) ;
#82105=CARTESIAN_POINT ( 'NONE',  ( 34.49999999999975131, 19.08746187583905751, 4.000000000000000000 ) ) ;
#82106=CARTESIAN_POINT ( 'NONE',  ( -8.999999999999934275, -19.22509904557637128, 1.855685503482156662 ) ) ;
#82107=EDGE_LOOP ( 'NONE', ( #41633, #60176, #35514, #25997 ) ) ;
#82108=DIRECTION ( 'NONE',  ( 0.000000000000000000, 1.000000000000000000, 0.000000000000000000 ) ) ;
#82110=DIRECTION ( 'NONE',  ( 0.7071067811865487940, 0.7071067811865463515, 0.000000000000000000 ) ) ;
#82111=VECTOR ( 'NONE', #127976, 1000.000000000000000 ) ;
#82113=ADVANCED_FACE ( 'NONE', ( #38161 ), #71495, .F. ) ;
#82114=EDGE_LOOP ( 'NONE', ( #70578, #129236, #32081, #80205 ) ) ;
#82116=CARTESIAN_POINT ( 'NONE',  ( 21.48921356237309155, -27.52281430457070499, 5.000000000000000000 ) ) ;
#82117=ORIENTED_EDGE ( 'NONE', *, *, #114734, .T. ) ;
#82119=DIRECTION ( 'NONE',  ( -0.3543493200069162685, -0.000000000000000000, -0.9351131265310288487 ) ) ;
#82123=ADVANCED_FACE ( 'NONE', ( #31560 ), #33721, .F. ) ;
#82125=CARTESIAN_POINT ( 'NONE',  ( 36.18398860626899705, 28.73617430169812437, 5.000000000000000000 ) ) ;
#82126=EDGE_CURVE ( 'NONE', #101548, #29429, #132326, .T. ) ;
#82127=CARTESIAN_POINT ( 'NONE',  ( -66.18398860626901126, 28.73617430169833753, 5.000000000000000000 ) ) ;
#82128=CARTESIAN_POINT ( 'NONE',  ( 19.17183060077633172, -5.240707523384232402, 4.000000000000000000 ) ) ;
#82129=CARTESIAN_POINT ( 'NONE',  ( 34.49999999999975131, 12.43112307739206024, 4.000000000000000000 ) ) ;
#82132=CARTESIAN_POINT ( 'NONE',  ( 30.18398860626900060, 28.73617430169808173, 5.000000000000000000 ) ) ;
#82133=DIRECTION ( 'NONE',  ( 0.7071067811865487940, 0.7071067811865463515, -0.000000000000000000 ) ) ;
#82135=VERTEX_POINT ( 'NONE', #98930 ) ;
#82136=CARTESIAN_POINT ( 'NONE',  ( 60.48921356237309510, -27.52281430457097500, 5.000000000000000000 ) ) ;
#82137=ORIENTED_EDGE ( 'NONE', *, *, #83151, .F. ) ;
#82138=ADVANCED_FACE ( 'NONE', ( #33018 ), #109825, .T. ) ;
#82141=ORIENTED_EDGE ( 'NONE', *, *, #37226, .T. ) ;
#82142=DIRECTION ( 'NONE',  ( -0.7071067811865487940, 0.7071067811865463515, 0.000000000000000000 ) ) ;
#82144=FACE_BOUND ( 'NONE', #65402, .T. ) ;
#82145=DIRECTION ( 'NONE',  ( -0.3543493200069162685, -0.000000000000000000, -0.9351131265310288487 ) ) ;
#82146=LINE ( 'NONE', #60388, #16693 ) ;
#82147=DIRECTION ( 'NONE',  ( 0.7071067811865486830, -0.7071067811865464625, -0.000000000000000000 ) ) ;
#82148=DIRECTION ( 'NONE',  ( 1.000000000000000000, 0.000000000000000000, 0.000000000000000000 ) ) ;
#82149=DIRECTION ( 'NONE',  ( 0.7071067811865486830, -0.7071067811865464625, -0.000000000000000000 ) ) ;
#82150=VERTEX_POINT ( 'NONE', #22768 ) ;
#82151=VECTOR ( 'NONE', #70596, 1000.000000000000000 ) ;
#82152=DIRECTION ( 'NONE',  ( 1.000000000000000000, 0.000000000000000000, 0.000000000000000000 ) ) ;
#82153=ORIENTED_EDGE ( 'NONE', *, *, #78190, .F. ) ;
#82154=VECTOR ( 'NONE', #7317, 1000.000000000000000 ) ;
#82155=EDGE_CURVE ( 'NONE', #134004, #29420, #88082, .T. ) ;
#82156=ORIENTED_EDGE ( 'NONE', *, *, #14636, .F. ) ;
#82158=ORIENTED_EDGE ( 'NONE', *, *, #39293, .F. ) ;
#82159=DIRECTION ( 'NONE',  ( -0.000000000000000000, 0.3543493200069153248, 0.9351131265310292928 ) ) ;
#82160=EDGE_CURVE ( 'NONE', #52188, #8725, #110509, .T. ) ;
#82162=CARTESIAN_POINT ( 'NONE',  ( 8.206660635421465955, 21.75929247661549226, 4.998822639870702744 ) ) ;
#82163=VERTEX_POINT ( 'NONE', #9787 ) ;
#82165=EDGE_CURVE ( 'NONE', #71270, #85690, #86664, .T. ) ;
#82166=EDGE_CURVE ( 'NONE', #20488, #45231, #109096, .T. ) ;
#82167=VECTOR ( 'NONE', #48306, 1000.000000000000000 ) ;
#82168=CARTESIAN_POINT ( 'NONE',  ( 42.48921356237308800, -27.52281430457085065, 5.000000000000000000 ) ) ;
#82169=CARTESIAN_POINT ( 'NONE',  ( 51.48921356237309510, -27.52281430457091460, 5.000000000000000000 ) ) ;
#82170=DIRECTION ( 'NONE',  ( 1.000000000000000000, 0.000000000000000000, 0.000000000000000000 ) ) ;
#82173=ORIENTED_EDGE ( 'NONE', *, *, #49774, .T. ) ;
#82174=CARTESIAN_POINT ( 'NONE',  ( 24.29974487139158867, -27.71228299555223273, 4.000000000000000000 ) ) ;
#82175=DIRECTION ( 'NONE',  ( 0.3543493200069162685, -0.000000000000000000, -0.9351131265310288487 ) ) ;
#82176=EDGE_LOOP ( 'NONE', ( #20797, #54105, #50010, #48947 ) ) ;
#82177=ORIENTED_EDGE ( 'NONE', *, *, #71991, .T. ) ;
#82178=ORIENTED_EDGE ( 'NONE', *, *, #9737, .F. ) ;
#82179=CARTESIAN_POINT ( 'NONE',  ( -19.05000000000000071, 3.174999999999997158, 4.000000000000000000 ) ) ;
#82180=EDGE_CURVE ( 'NONE', #24024, #85105, #141009, .T. ) ;
#82182=DIRECTION ( 'NONE',  ( 0.3543493200069162685, -0.000000000000000000, -0.9351131265310288487 ) ) ;
#82183=ORIENTED_EDGE ( 'NONE', *, *, #122434, .T. ) ;
#82184=CARTESIAN_POINT ( 'NONE',  ( -2.218373117075048029, 21.74787736706806385, 4.999607392498049308 ) ) ;
#82185=EDGE_CURVE ( 'NONE', #106062, #64397, #35149, .T. ) ;
#82187=DIRECTION ( 'NONE',  ( 0.3543493200069162685, -0.000000000000000000, -0.9351131265310288487 ) ) ;
#82188=VECTOR ( 'NONE', #79903, 1000.000000000000000 ) ;
#82190=VECTOR ( 'NONE', #122989, 1000.000000000000227 ) ;
#82191=PLANE ( 'NONE',  #123624 ) ;
#82194=CARTESIAN_POINT ( 'NONE',  ( -5.700255128608413102, -27.71228299555201957, 4.000000000000000000 ) ) ;
#82195=CARTESIAN_POINT ( 'NONE',  ( -29.99999999999979394, -19.22509904557638905, 1.855685503482108256 ) ) ;
#82196=EDGE_CURVE ( 'NONE', #133600, #16078, #114109, .T. ) ;
#82198=ORIENTED_EDGE ( 'NONE', *, *, #113757, .T. ) ;
#82199=DIRECTION ( 'NONE',  ( -0.000000000000000000, -0.3543493200069152693, 0.9351131265310292928 ) ) ;
#82200=ORIENTED_EDGE ( 'NONE', *, *, #36112, .F. ) ;
#82201=LINE ( 'NONE', #60445, #86628 ) ;
#82202=CARTESIAN_POINT ( 'NONE',  ( 34.92499999999998295, 0.6624618758390189432, 4.000000000000000000 ) ) ;
#82203=PLANE ( 'NONE',  #54030 ) ;
#82204=ORIENTED_EDGE ( 'NONE', *, *, #14565, .F. ) ;
#82206=CARTESIAN_POINT ( 'NONE',  ( 13.49999999999990763, 18.05218569542898521, 5.000000000000000000 ) ) ;
#82208=FACE_OUTER_BOUND ( 'NONE', #142711, .T. ) ;
#82209=EDGE_CURVE ( 'NONE', #75880, #23207, #69938, .T. ) ;
#82211=LINE ( 'NONE', #18305, #53145 ) ;
#82212=CARTESIAN_POINT ( 'NONE',  ( -17.99999999999987566, 11.58746187583913390, 4.000000000000000000 ) ) ;
#82214=CARTESIAN_POINT ( 'NONE',  ( -6.183988606268994381, 28.73617430169791476, 5.000000000000000000 ) ) ;
#82215=LINE ( 'NONE', #116941, #120021 ) ;
#82217=ADVANCED_FACE ( 'NONE', ( #12640 ), #47478, .F. ) ;
#82218=VERTEX_POINT ( 'NONE', #100391 ) ;
#82219=CARTESIAN_POINT ( 'NONE',  ( -2.292893218813443657, 8.259292476615634371, 5.000000000000000000 ) ) ;
#82220=PLANE ( 'NONE',  #85333 ) ;
#82221=EDGE_CURVE ( 'NONE', #108587, #104249, #34409, .T. ) ;
#82223=DIRECTION ( 'NONE',  ( -0.3543493200069162685, -0.000000000000000000, -0.9351131265310288487 ) ) ;
#82224=LINE ( 'NONE', #14788, #50770 ) ;
#82225=CARTESIAN_POINT ( 'NONE',  ( -0.2392503087990174859, 22.22500000000000142, -8.143727179408113415 ) ) ;
#82226=DIRECTION ( 'NONE',  ( 0.7071067811865487940, 0.7071067811865463515, 0.000000000000000000 ) ) ;
#82228=DIRECTION ( 'NONE',  ( -0.7071067811865486830, -0.7071067811865464625, 0.000000000000000000 ) ) ;
#82229=PLANE ( 'NONE',  #88670 ) ;
#82232=PLANE ( 'NONE',  #71950 ) ;
#82233=EDGE_LOOP ( 'NONE', ( #12980, #8975, #109183, #30082 ) ) ;
#82234=PLANE ( 'NONE',  #62734 ) ;
#82235=VERTEX_POINT ( 'NONE', #123596 ) ;
#82236=ORIENTED_EDGE ( 'NONE', *, *, #111587, .T. ) ;
#82237=FACE_OUTER_BOUND ( 'NONE', #101408, .T. ) ;
#82238=DIRECTION ( 'NONE',  ( -0.7071067811865487940, 0.7071067811865463515, 0.000000000000000000 ) ) ;
#82239=FACE_OUTER_BOUND ( 'NONE', #95938, .T. ) ;
#82240=FACE_OUTER_BOUND ( 'NONE', #118937, .T. ) ;
#82241=LINE ( 'NONE', #115507, #132098 ) ;
#82242=DIRECTION ( 'NONE',  ( 0.7071067811865487940, 0.7071067811865463515, -0.000000000000000000 ) ) ;
#82245=LINE ( 'NONE', #116273, #60745 ) ;
#82247=CARTESIAN_POINT ( 'NONE',  ( -34.92500000000001137, -15.28150956279560191, 4.759050581649335143 ) ) ;
#82248=DIRECTION ( 'NONE',  ( -0.000000000000000000, 0.000000000000000000, 1.000000000000000000 ) ) ;
#82251=VECTOR ( 'NONE', #81011, 1000.000000000000000 ) ;
#82254=VERTEX_POINT ( 'NONE', #102542 ) ;
#82256=CARTESIAN_POINT ( 'NONE',  ( -0.5240013858544890768, 22.03583458319438648, 4.979811245910087614 ) ) ;
#82257=VECTOR ( 'NONE', #102403, 999.9999999999998863 ) ;
#82258=DIRECTION ( 'NONE',  ( 0.7071067811865487940, 0.7071067811865463515, 0.000000000000000000 ) ) ;
#82259=DIRECTION ( 'NONE',  ( 0.000000000000000000, 1.000000000000000000, -0.000000000000000000 ) ) ;
#82260=ORIENTED_EDGE ( 'NONE', *, *, #99785, .F. ) ;
#82261=FACE_OUTER_BOUND ( 'NONE', #96068, .T. ) ;
#82262=VECTOR ( 'NONE', #128220, 1000.000000000000000 ) ;
#82265=PLANE ( 'NONE',  #11211 ) ;
#82266=ORIENTED_EDGE ( 'NONE', *, *, #81051, .T. ) ;
#82267=VERTEX_POINT ( 'NONE', #68498 ) ;
#82268=CARTESIAN_POINT ( 'NONE',  ( -35.95341186370433206, 14.25929247661557042, 18.84478104361335937 ) ) ;
#82269=CARTESIAN_POINT ( 'NONE',  ( 0.000000000000000000, 0.000000000000000000, 5.000000000000000000 ) ) ;
#82270=CARTESIAN_POINT ( 'NONE',  ( -4.499999999999964473, 0.05218569542916884352, 5.000000000000000000 ) ) ;
#82271=ADVANCED_FACE ( 'NONE', ( #92330 ), #46023, .T. ) ;
#82272=DIRECTION ( 'NONE',  ( -0.6830127018922181881, 0.6830127018922202975, -0.2588190451025214056 ) ) ;
#82273=CARTESIAN_POINT ( 'NONE',  ( -34.49999999999975842, 16.18958161055400069, -11.56426086740819414 ) ) ;
#82274=ORIENTED_EDGE ( 'NONE', *, *, #64686, .T. ) ;
#82277=PLANE ( 'NONE',  #47829 ) ;
#82278=CARTESIAN_POINT ( 'NONE',  ( -48.48921356237309510, -27.52281430457089328, 5.000000000000000000 ) ) ;
#82279=DIRECTION ( 'NONE',  ( -0.7071067811865487940, 0.7071067811865463515, -0.000000000000000000 ) ) ;
#82280=VECTOR ( 'NONE', #135407, 1000.000000000000227 ) ;
#82281=ORIENTED_EDGE ( 'NONE', *, *, #122794, .T. ) ;
#82282=ORIENTED_EDGE ( 'NONE', *, *, #9012, .F. ) ;
#82284=EDGE_CURVE ( 'NONE', #35225, #48229, #78632, .T. ) ;
#82285=DIRECTION ( 'NONE',  ( -0.000000000000000000, -0.3543493200069152693, 0.9351131265310292928 ) ) ;
#82286=CARTESIAN_POINT ( 'NONE',  ( -38.99451991528749062, 28.92564299267965211, 4.000000000000000000 ) ) ;
#82287=PLANE ( 'NONE',  #135764 ) ;
#82289=ORIENTED_EDGE ( 'NONE', *, *, #53124, .F. ) ;
#82291=FACE_OUTER_BOUND ( 'NONE', #65977, .T. ) ;
#82292=FACE_OUTER_BOUND ( 'NONE', #57714, .T. ) ;
#82294=ORIENTED_EDGE ( 'NONE', *, *, #4713, .F. ) ;
#82295=LINE ( 'NONE', #143076, #2754 ) ;
#82296=ORIENTED_EDGE ( 'NONE', *, *, #599, .F. ) ;
#82297=CARTESIAN_POINT ( 'NONE',  ( 66.29974487139159578, -27.71228299555252406, 4.000000000000000000 ) ) ;
#82298=DIRECTION ( 'NONE',  ( -0.7071067811865486830, -0.7071067811865464625, 0.000000000000000000 ) ) ;
#82299=EDGE_CURVE ( 'NONE', #106502, #32200, #90953, .T. ) ;
#82300=FACE_BOUND ( 'NONE', #39165, .T. ) ;
#82302=CARTESIAN_POINT ( 'NONE',  ( -2.862559987030901976, 22.22500000000000142, -7.149657077860686272 ) ) ;
#82303=DIRECTION ( 'NONE',  ( -0.7071067811865487940, 0.7071067811865463515, -0.000000000000000000 ) ) ;
#82304=PLANE ( 'NONE',  #48194 ) ;
#82305=FACE_OUTER_BOUND ( 'NONE', #8220, .T. ) ;
#82308=VERTEX_POINT ( 'NONE', #57614 ) ;
#82311=DIRECTION ( 'NONE',  ( 0.7071067811865487940, 0.7071067811865463515, 0.000000000000000000 ) ) ;
#82312=ADVANCED_FACE ( 'NONE', ( #35874 ), #80090, .F. ) ;
#82313=CARTESIAN_POINT ( 'NONE',  ( -26.99999999999980815, -6.412538124160691133, 4.000000000000000000 ) ) ;
#82314=EDGE_CURVE ( 'NONE', #59374, #45046, #62594, .T. ) ;
#82315=ADVANCED_FACE ( 'NONE', ( #17623 ), #95197, .F. ) ;
#82316=DIRECTION ( 'NONE',  ( 0.7071067811865487940, 0.7071067811865463515, 0.000000000000000000 ) ) ;
#82317=VERTEX_POINT ( 'NONE', #6016 ) ;
#82318=LINE ( 'NONE', #126499, #18231 ) ;
#82319=LINE ( 'NONE', #16295, #20004 ) ;
#82320=PLANE ( 'NONE',  #131481 ) ;
#82322=CARTESIAN_POINT ( 'NONE',  ( 42.48921356237308800, -27.52281430457085065, 5.000000000000000000 ) ) ;
#82323=LINE ( 'NONE', #126505, #88641 ) ;
#82324=DIRECTION ( 'NONE',  ( -0.7071067811865486830, 0.7071067811865464625, 0.000000000000000000 ) ) ;
#82325=CARTESIAN_POINT ( 'NONE',  ( -12.00548008471251293, 28.92564299267929684, 4.000000000000000000 ) ) ;
#82326=ORIENTED_EDGE ( 'NONE', *, *, #113823, .T. ) ;
#82327=ADVANCED_FACE ( 'NONE', ( #105359 ), #61215, .F. ) ;
#82328=CARTESIAN_POINT ( 'NONE',  ( -41.99451991528749062, 28.92564299267967343, 4.000000000000000000 ) ) ;
#82330=ORIENTED_EDGE ( 'NONE', *, *, #49297, .F. ) ;
#82331=ORIENTED_EDGE ( 'NONE', *, *, #118444, .T. ) ;
#82332=EDGE_CURVE ( 'NONE', #26466, #29361, #29934, .T. ) ;
#82333=EDGE_CURVE ( 'NONE', #43201, #20344, #117636, .T. ) ;
#82334=EDGE_LOOP ( 'NONE', ( #35073, #5007, #98222, #33896, #106342, #26887 ) ) ;
#82336=VERTEX_POINT ( 'NONE', #15467 ) ;
#82337=VECTOR ( 'NONE', #126449, 999.9999999999998863 ) ;
#82342=EDGE_CURVE ( 'NONE', #18045, #108455, #140158, .T. ) ;
#82343=ORIENTED_EDGE ( 'NONE', *, *, #75523, .T. ) ;
#82347=FACE_OUTER_BOUND ( 'NONE', #17368, .T. ) ;
#82349=EDGE_CURVE ( 'NONE', #52857, #15815, #27090, .T. ) ;
#82350=LINE ( 'NONE', #62742, #33235 ) ;
#82351=ORIENTED_EDGE ( 'NONE', *, *, #113199, .F. ) ;
#82352=ORIENTED_EDGE ( 'NONE', *, *, #79326, .F. ) ;
#82354=ORIENTED_EDGE ( 'NONE', *, *, #75822, .T. ) ;
#82355=LINE ( 'NONE', #138875, #27265 ) ;
#82356=ORIENTED_EDGE ( 'NONE', *, *, #91976, .T. ) ;
#82358=ORIENTED_EDGE ( 'NONE', *, *, #139893, .T. ) ;
#82359=VERTEX_POINT ( 'NONE', #72075 ) ;
#82360=ORIENTED_EDGE ( 'NONE', *, *, #15863, .T. ) ;
#82361=CARTESIAN_POINT ( 'NONE',  ( 10.49999999999993960, 22.08746187583901843, 4.000000000000000000 ) ) ;
#82362=CARTESIAN_POINT ( 'NONE',  ( -2.510786437626908008, -27.52281430457053446, 5.000000000000000000 ) ) ;
#82363=CARTESIAN_POINT ( 'NONE',  ( 63.48921356237309510, -27.52281430457099631, 5.000000000000000000 ) ) ;
#82364=LINE ( 'NONE', #117094, #127079 ) ;
#82365=DIRECTION ( 'NONE',  ( 0.7071067811865486830, -0.7071067811865464625, -0.000000000000000000 ) ) ;
#82366=ORIENTED_EDGE ( 'NONE', *, *, #139243, .F. ) ;
#82367=FACE_OUTER_BOUND ( 'NONE', #15489, .T. ) ;
#82368=VECTOR ( 'NONE', #35210, 1000.000000000000227 ) ;
#82369=EDGE_CURVE ( 'NONE', #39996, #69883, #50293, .T. ) ;
#82370=ADVANCED_FACE ( 'NONE', ( #106051 ), #61894, .F. ) ;
#82373=FACE_OUTER_BOUND ( 'NONE', #19969, .T. ) ;
#82374=AXIS2_PLACEMENT_3D ( 'NONE', #26186, #24040, #58866 ) ;
#82375=CARTESIAN_POINT ( 'NONE',  ( -8.999999999999941380, -0.8619312979532035568, -5.102805207349846661 ) ) ;
#82376=ORIENTED_EDGE ( 'NONE', *, *, #50279, .T. ) ;
#82377=ORIENTED_EDGE ( 'NONE', *, *, #126321, .F. ) ;
#82378=ORIENTED_EDGE ( 'NONE', *, *, #33248, .T. ) ;
#82379=CARTESIAN_POINT ( 'NONE',  ( -19.82816939922339827, 12.75929247661558286, 4.000000000000000000 ) ) ;
#82380=LINE ( 'NONE', #59912, #7043 ) ;
#82382=DIRECTION ( 'NONE',  ( -0.7071067811865486830, 0.7071067811865464625, 0.000000000000000000 ) ) ;
#82383=VECTOR ( 'NONE', #33037, 1000.000000000000000 ) ;
#82385=EDGE_CURVE ( 'NONE', #59942, #32191, #137303, .T. ) ;
#82386=LINE ( 'NONE', #79566, #59845 ) ;
#82388=CARTESIAN_POINT ( 'NONE',  ( -69.18398860626899705, 28.73617430169835529, 5.000000000000000000 ) ) ;
#82389=DIRECTION ( 'NONE',  ( -0.3543493200069162685, -0.000000000000000000, -0.9351131265310288487 ) ) ;
#82390=LINE ( 'NONE', #126568, #104565 ) ;
#82391=LINE ( 'NONE', #59924, #88157 ) ;
#82392=ORIENTED_EDGE ( 'NONE', *, *, #50804, .T. ) ;
#82394=ORIENTED_EDGE ( 'NONE', *, *, #123462, .T. ) ;
#82395=CARTESIAN_POINT ( 'NONE',  ( -33.29974487139158867, -27.71228299555229313, 4.000000000000000000 ) ) ;
#82396=DIRECTION ( 'NONE',  ( -0.6830127018922181881, 0.6830127018922202975, -0.2588190451025214056 ) ) ;
#82397=ORIENTED_EDGE ( 'NONE', *, *, #122335, .F. ) ;
#82398=DIRECTION ( 'NONE',  ( 0.000000000000000000, 1.000000000000000000, 0.000000000000000000 ) ) ;
#82399=LINE ( 'NONE', #40339, #128230 ) ;
#82401=LINE ( 'NONE', #132156, #57750 ) ;
#82402=ORIENTED_EDGE ( 'NONE', *, *, #103841, .F. ) ;
#82405=DIRECTION ( 'NONE',  ( -0.6830127018922181881, 0.6830127018922202975, -0.2588190451025214056 ) ) ;
#82407=DIRECTION ( 'NONE',  ( -0.000000000000000000, 0.000000000000000000, 1.000000000000000000 ) ) ;
#82408=CARTESIAN_POINT ( 'NONE',  ( -21.18398860626899349, 28.73617430169802134, 5.000000000000000000 ) ) ;
#82409=ORIENTED_EDGE ( 'NONE', *, *, #103610, .F. ) ;
#82410=DIRECTION ( 'NONE',  ( -0.7071067811865486830, 0.7071067811865464625, 0.000000000000000000 ) ) ;
#82411=ADVANCED_FACE ( 'NONE', ( #116248 ), #127862, .F. ) ;
#82412=DIRECTION ( 'NONE',  ( -0.000000000000000000, 0.3543493200069153248, 0.9351131265310292928 ) ) ;
#82415=DIRECTION ( 'NONE',  ( -0.7071067811865486830, -0.7071067811865464625, 0.000000000000000000 ) ) ;
#82416=EDGE_LOOP ( 'NONE', ( #84348, #123997, #61880, #119895 ) ) ;
#82417=CARTESIAN_POINT ( 'NONE',  ( -15.72281430457048934, -21.72500000000000497, 5.000000000000000000 ) ) ;
#82418=ORIENTED_EDGE ( 'NONE', *, *, #43528, .F. ) ;
#82420=DIRECTION ( 'NONE',  ( 0.7071067811865487940, -0.7071067811865463515, 0.000000000000000000 ) ) ;
#82421=CARTESIAN_POINT ( 'NONE',  ( 21.29974487139158512, -27.71228299555221142, 4.000000000000000000 ) ) ;
#82422=PLANE ( 'NONE',  #3865 ) ;
#82423=ORIENTED_EDGE ( 'NONE', *, *, #117436, .T. ) ;
#82424=CARTESIAN_POINT ( 'NONE',  ( 30.29974487139158867, -27.71228299555227537, 4.000000000000000000 ) ) ;
#82425=ADVANCED_FACE ( 'NONE', ( #39421 ), #51002, .F. ) ;
#82426=DIRECTION ( 'NONE',  ( 0.7071067811865487940, 0.7071067811865463515, 0.000000000000000000 ) ) ;
#82428=EDGE_CURVE ( 'NONE', #82613, #85586, #6718, .T. ) ;
#82431=ORIENTED_EDGE ( 'NONE', *, *, #73598, .F. ) ;
#82435=DIRECTION ( 'NONE',  ( -0.6830127018922181881, 0.6830127018922202975, -0.2588190451025214056 ) ) ;
#82438=ORIENTED_EDGE ( 'NONE', *, *, #132007, .T. ) ;
#82440=VERTEX_POINT ( 'NONE', #121230 ) ;
#82444=VECTOR ( 'NONE', #66236, 1000.000000000000000 ) ;
#82445=ADVANCED_FACE ( 'NONE', ( #64723 ), #108186, .F. ) ;
#82446=DIRECTION ( 'NONE',  ( -0.000000000000000000, 0.3543493200069153248, 0.9351131265310292928 ) ) ;
#82447=PLANE ( 'NONE',  #15505 ) ;
#82448=CARTESIAN_POINT ( 'NONE',  ( -60.29974487139158867, -27.71228299555248142, 4.000000000000000000 ) ) ;
#82449=LINE ( 'NONE', #41072, #131412 ) ;
#82451=LINE ( 'NONE', #73704, #83867 ) ;
#82452=LINE ( 'NONE', #139708, #141632 ) ;
#82453=EDGE_CURVE ( 'NONE', #95640, #141807, #11016, .T. ) ;
#82454=ORIENTED_EDGE ( 'NONE', *, *, #91636, .F. ) ;
#82455=VECTOR ( 'NONE', #82242, 1000.000000000000000 ) ;
#82456=LINE ( 'NONE', #62134, #72155 ) ;
#82457=FACE_OUTER_BOUND ( 'NONE', #133335, .T. ) ;
#82459=EDGE_CURVE ( 'NONE', #81462, #34037, #39548, .T. ) ;
#82461=ORIENTED_EDGE ( 'NONE', *, *, #54220, .F. ) ;
#82462=CARTESIAN_POINT ( 'NONE',  ( 24.72281430457042717, -21.72500000000000142, 5.000000000000000000 ) ) ;
#82463=CARTESIAN_POINT ( 'NONE',  ( 15.48921356237309510, -27.52281430457066236, 5.000000000000000000 ) ) ;
#82464=DIRECTION ( 'NONE',  ( -0.000000000000000000, -0.3543493200069152693, 0.9351131265310292928 ) ) ;
#82465=LINE ( 'NONE', #27338, #49023 ) ;
#82467=VECTOR ( 'NONE', #114004, 1000.000000000000000 ) ;
#82469=LINE ( 'NONE', #72346, #72069 ) ;
#82470=ORIENTED_EDGE ( 'NONE', *, *, #82155, .T. ) ;
#82471=AXIS2_PLACEMENT_3D ( 'NONE', #26108, #6421, #49311 ) ;
#82472=ORIENTED_EDGE ( 'NONE', *, *, #123840, .F. ) ;
#82473=ORIENTED_EDGE ( 'NONE', *, *, #88055, .F. ) ;
#82474=VECTOR ( 'NONE', #60329, 1000.000000000000000 ) ;
#82476=ADVANCED_FACE ( 'NONE', ( #42989 ), #87189, .F. ) ;
#82477=VECTOR ( 'NONE', #121070, 1000.000000000000227 ) ;
#82479=ADVANCED_FACE ( 'NONE', ( #76322 ), #109648, .T. ) ;
#82480=ORIENTED_EDGE ( 'NONE', *, *, #80849, .T. ) ;
#82482=LINE ( 'NONE', #48413, #49538 ) ;
#82483=EDGE_CURVE ( 'NONE', #22968, #54633, #131, .T. ) ;
#82484=CARTESIAN_POINT ( 'NONE',  ( -10.82816939922345512, 0.7592924766157138627, 4.000000000000000000 ) ) ;
#82487=ADVANCED_FACE ( 'NONE', ( #99460 ), #132865, .F. ) ;
#82488=FACE_OUTER_BOUND ( 'NONE', #104145, .T. ) ;
#82490=ORIENTED_EDGE ( 'NONE', *, *, #96849, .T. ) ;
#82491=CARTESIAN_POINT ( 'NONE',  ( -27.18398860626900060, 28.73617430169806042, 5.000000000000000000 ) ) ;
#82492=VERTEX_POINT ( 'NONE', #32832 ) ;
#82493=ORIENTED_EDGE ( 'NONE', *, *, #88710, .F. ) ;
#82494=CARTESIAN_POINT ( 'NONE',  ( 23.29289321881329755, -3.740707523384243505, 5.000000000000000000 ) ) ;
#82495=EDGE_LOOP ( 'NONE', ( #119478, #36675, #136624, #35457 ) ) ;
#82496=VERTEX_POINT ( 'NONE', #77055 ) ;
#82498=EDGE_LOOP ( 'NONE', ( #131767, #115038, #92622, #138685, #84775 ) ) ;
#82500=LINE ( 'NONE', #7764, #114430 ) ;
#82502=DIRECTION ( 'NONE',  ( -0.7071067811865486830, -0.7071067811865464625, -0.000000000000000000 ) ) ;
#82503=EDGE_CURVE ( 'NONE', #23195, #32169, #33555, .T. ) ;
#82504=DIRECTION ( 'NONE',  ( 1.000000000000000000, 0.000000000000000000, 0.000000000000000000 ) ) ;
#82505=LINE ( 'NONE', #22548, #62581 ) ;
#82506=AXIS2_PLACEMENT_3D ( 'NONE', #47359, #14669, #77284 ) ;
#82508=CARTESIAN_POINT ( 'NONE',  ( 34.42499999999998295, -21.72500000000000142, 5.000000000000000000 ) ) ;
#82509=CARTESIAN_POINT ( 'NONE',  ( -74.99451991528749772, 28.92564299267990435, 4.000000000000000000 ) ) ;
#82510=CARTESIAN_POINT ( 'NONE',  ( 19.82816939922339472, -8.240707523384191546, 4.000000000000000000 ) ) ;
#82512=PLANE ( 'NONE',  #61976 ) ;
#82514=ORIENTED_EDGE ( 'NONE', *, *, #78589, .T. ) ;
#82516=VECTOR ( 'NONE', #46037, 1000.000000000000227 ) ;
#82518=EDGE_LOOP ( 'NONE', ( #96729, #99568, #53286, #137792 ) ) ;
#82519=DIRECTION ( 'NONE',  ( 0.7071067811865487940, 0.7071067811865463515, 0.000000000000000000 ) ) ;
#82520=CARTESIAN_POINT ( 'NONE',  ( -32.67183060077623935, -9.740707523384180888, 4.000000000000000000 ) ) ;
#82521=PLANE ( 'NONE',  #94917 ) ;
#82524=DIRECTION ( 'NONE',  ( 0.7071067811865487940, -0.7071067811865463515, -0.000000000000000000 ) ) ;
#82526=LINE ( 'NONE', #126716, #21358 ) ;
#82528=EDGE_CURVE ( 'NONE', #1213, #97544, #46255, .T. ) ;
#82530=CARTESIAN_POINT ( 'NONE',  ( 34.92499999999997584, -15.28150956279557526, 4.759050581649322709 ) ) ;
#82531=CARTESIAN_POINT ( 'NONE',  ( -2.292893218813438772, -6.740707523384212863, 5.000000000000000000 ) ) ;
#82533=CARTESIAN_POINT ( 'NONE',  ( 26.99451991528749417, 28.92564299267956685, 4.000000000000000000 ) ) ;
#82534=ORIENTED_EDGE ( 'NONE', *, *, #89505, .T. ) ;
#82535=ORIENTED_EDGE ( 'NONE', *, *, #31902, .F. ) ;
#82536=ORIENTED_EDGE ( 'NONE', *, *, #142207, .F. ) ;
#82538=DIRECTION ( 'NONE',  ( 0.7071067811865487940, 0.7071067811865463515, -0.000000000000000000 ) ) ;
#82539=PLANE ( 'NONE',  #10318 ) ;
#82540=DIRECTION ( 'NONE',  ( -0.7071067811865486830, -0.7071067811865464625, 0.000000000000000000 ) ) ;
#82541=DIRECTION ( 'NONE',  ( -0.7071067811865487940, 0.7071067811865463515, -0.000000000000000000 ) ) ;
#82542=LINE ( 'NONE', #5661, #138371 ) ;
#82543=FACE_OUTER_BOUND ( 'NONE', #52718, .T. ) ;
#82544=VECTOR ( 'NONE', #61470, 1000.000000000000000 ) ;
#82545=CARTESIAN_POINT ( 'NONE',  ( 21.18398860626899349, 28.73617430169802134, 5.000000000000000000 ) ) ;
#82546=DIRECTION ( 'NONE',  ( -0.7071067811865486830, -0.7071067811865464625, 0.000000000000000000 ) ) ;
#82547=ORIENTED_EDGE ( 'NONE', *, *, #11625, .T. ) ;
#82549=DIRECTION ( 'NONE',  ( 0.6830127018922180770, -0.6830127018922204085, -0.2588190451025213501 ) ) ;
#82551=CARTESIAN_POINT ( 'NONE',  ( -5.200031220168336077, 8.259292476615634371, 16.85664084051842337 ) ) ;
#82555=EDGE_LOOP ( 'NONE', ( #10171, #11966, #38858, #129899, #48918 ) ) ;
#82556=LINE ( 'NONE', #17966, #44580 ) ;
#82557=CARTESIAN_POINT ( 'NONE',  ( -23.99999999999981881, 20.58746187583902909, 4.000000000000000000 ) ) ;
#82558=LINE ( 'NONE', #126747, #127043 ) ;
#82559=ORIENTED_EDGE ( 'NONE', *, *, #41042, .F. ) ;
#82560=CARTESIAN_POINT ( 'NONE',  ( 0.000000000000000000, 0.000000000000000000, 5.000000000000000000 ) ) ;
#82561=ORIENTED_EDGE ( 'NONE', *, *, #53020, .F. ) ;
#82562=AXIS2_PLACEMENT_3D ( 'NONE', #84262, #127748, #50188 ) ;
#82563=AXIS2_PLACEMENT_3D ( 'NONE', #67690, #12543, #120563 ) ;
#82567=DIRECTION ( 'NONE',  ( 0.6830127018922180770, -0.6830127018922204085, -0.2588190451025213501 ) ) ;
#82568=LINE ( 'NONE', #126760, #108714 ) ;
#82569=DIRECTION ( 'NONE',  ( -0.000000000000000000, 0.000000000000000000, 1.000000000000000000 ) ) ;
#82571=CARTESIAN_POINT ( 'NONE',  ( 13.49999999999991118, -7.912538124160675146, 4.000000000000000000 ) ) ;
#82574=DIRECTION ( 'NONE',  ( -0.000000000000000000, -0.3543493200069152693, 0.9351131265310292928 ) ) ;
#82575=LINE ( 'NONE', #58740, #127701 ) ;
#82576=LINE ( 'NONE', #22273, #128817 ) ;
#82577=ORIENTED_EDGE ( 'NONE', *, *, #16898, .F. ) ;
#82578=ORIENTED_EDGE ( 'NONE', *, *, #41255, .F. ) ;
#82580=DIRECTION ( 'NONE',  ( -0.000000000000000000, 0.000000000000000000, 1.000000000000000000 ) ) ;
#82581=ORIENTED_EDGE ( 'NONE', *, *, #89872, .T. ) ;
#82582=ORIENTED_EDGE ( 'NONE', *, *, #65776, .F. ) ;
#82583=EDGE_CURVE ( 'NONE', #79492, #55124, #67610, .T. ) ;
#82584=CARTESIAN_POINT ( 'NONE',  ( -34.17183060077623225, 18.75929247661552779, 4.000000000000000000 ) ) ;
#82585=LINE ( 'NONE', #27461, #126624 ) ;
#82586=ORIENTED_EDGE ( 'NONE', *, *, #35406, .T. ) ;
#82587=LINE ( 'NONE', #115891, #97221 ) ;
#82588=CARTESIAN_POINT ( 'NONE',  ( -26.29289321881326913, 5.259292476615661016, 5.000000000000000000 ) ) ;
#82589=DIRECTION ( 'NONE',  ( -0.7071067811865487940, 0.7071067811865463515, 0.000000000000000000 ) ) ;
#82591=EDGE_CURVE ( 'NONE', #76029, #50763, #3699, .T. ) ;
#82592=EDGE_CURVE ( 'NONE', #143132, #7428, #69024, .T. ) ;
#82593=CARTESIAN_POINT ( 'NONE',  ( 16.19018167574437683, -18.74070752338409562, 7.910009926591468954 ) ) ;
#82594=PLANE ( 'NONE',  #38151 ) ;
#82595=CARTESIAN_POINT ( 'NONE',  ( -39.18398860626899705, 28.73617430169814568, 5.000000000000000000 ) ) ;
#82596=LINE ( 'NONE', #4245, #112382 ) ;
#82597=DIRECTION ( 'NONE',  ( -0.6830127018922181881, 0.6830127018922202975, -0.2588190451025214056 ) ) ;
#82598=DIRECTION ( 'NONE',  ( -0.6830127018922181881, 0.6830127018922202975, -0.2588190451025214056 ) ) ;
#82599=DIRECTION ( 'NONE',  ( -0.7071067811865487940, 0.7071067811865463515, 0.000000000000000000 ) ) ;
#82600=FACE_OUTER_BOUND ( 'NONE', #63530, .T. ) ;
#82601=EDGE_CURVE ( 'NONE', #99505, #4103, #91483, .T. ) ;
#82602=EDGE_CURVE ( 'NONE', #110390, #16024, #47993, .T. ) ;
#82603=ORIENTED_EDGE ( 'NONE', *, *, #65379, .T. ) ;
#82604=EDGE_LOOP ( 'NONE', ( #116906, #32920, #46558, #42073 ) ) ;
#82608=EDGE_CURVE ( 'NONE', #56006, #141462, #113930, .T. ) ;
#82609=DIRECTION ( 'NONE',  ( 0.6830127018922181881, 0.6830127018922202975, -0.2588190451025214056 ) ) ;
#82611=ADVANCED_FACE ( 'NONE', ( #79212 ), #22604, .T. ) ;
#82613=VERTEX_POINT ( 'NONE', #2274 ) ;
#82614=DIRECTION ( 'NONE',  ( 0.6830127018922180770, -0.6830127018922204085, -0.2588190451025213501 ) ) ;
#82615=DIRECTION ( 'NONE',  ( -0.6830127018922181881, 0.6830127018922202975, -0.2588190451025214056 ) ) ;
#82619=VERTEX_POINT ( 'NONE', #122656 ) ;
#82620=DIRECTION ( 'NONE',  ( -0.000000000000000000, 0.000000000000000000, 1.000000000000000000 ) ) ;
#82621=ORIENTED_EDGE ( 'NONE', *, *, #128641, .F. ) ;
#82622=FACE_OUTER_BOUND ( 'NONE', #41689, .T. ) ;
#82623=VECTOR ( 'NONE', #121945, 1000.000000000000000 ) ;
#82624=DIRECTION ( 'NONE',  ( -0.000000000000000000, 0.3543493200069153248, 0.9351131265310292928 ) ) ;
#82625=DIRECTION ( 'NONE',  ( 0.7071067811865487940, 0.7071067811865463515, -0.000000000000000000 ) ) ;
#82626=EDGE_CURVE ( 'NONE', #71467, #77426, #25479, .T. ) ;
#82627=ORIENTED_EDGE ( 'NONE', *, *, #63844, .F. ) ;
#82628=ORIENTED_EDGE ( 'NONE', *, *, #65767, .T. ) ;
#82629=VECTOR ( 'NONE', #77667, 1000.000000000000000 ) ;
#82630=VERTEX_POINT ( 'NONE', #111800 ) ;
#82634=ADVANCED_FACE ( 'NONE', ( #23337 ), #862, .F. ) ;
#82635=CARTESIAN_POINT ( 'NONE',  ( 29.99999999999979750, -18.03360074219754949, 5.000000000000000000 ) ) ;
#82636=VECTOR ( 'NONE', #79146, 1000.000000000000000 ) ;
#82637=( NAMED_UNIT ( * ) SI_UNIT ( $, .STERADIAN. ) SOLID_ANGLE_UNIT ( ) );
#82638=CARTESIAN_POINT ( 'NONE',  ( -65.99451991528749772, 28.92564299267984396, 4.000000000000000000 ) ) ;
#82639=ORIENTED_EDGE ( 'NONE', *, *, #135622, .F. ) ;
#82640=AXIS2_PLACEMENT_3D ( 'NONE', #125065, #12725, #34497 ) ;
#82641=ORIENTED_EDGE ( 'NONE', *, *, #89408, .F. ) ;
#82642=FACE_OUTER_BOUND ( 'NONE', #128152, .T. ) ;
#82643=EDGE_LOOP ( 'NONE', ( #11693, #57203, #53126 ) ) ;
#82645=EDGE_CURVE ( 'NONE', #69514, #135832, #45851, .T. ) ;
#82646=DIRECTION ( 'NONE',  ( -0.7071067811865486830, -0.7071067811865464625, -0.000000000000000000 ) ) ;
#82647=ADVANCED_FACE ( 'NONE', ( #77754 ), #57439, .F. ) ;
#82648=LINE ( 'NONE', #116689, #5108 ) ;
#82649=CARTESIAN_POINT ( 'NONE',  ( 21.71715331601274102, -2.164967620583693630, 5.000000000000000000 ) ) ;
#82650=ORIENTED_EDGE ( 'NONE', *, *, #120816, .F. ) ;
#82652=EDGE_CURVE ( 'NONE', #26845, #11127, #34242, .T. ) ;
#82653=CARTESIAN_POINT ( 'NONE',  ( 12.18398860626900060, 28.73617430169795739, 5.000000000000000000 ) ) ;
#82654=LINE ( 'NONE', #105104, #138644 ) ;
#82655=EDGE_CURVE ( 'NONE', #91841, #26097, #34972, .T. ) ;
#82656=LINE ( 'NONE', #39887, #58294 ) ;
#82657=VERTEX_POINT ( 'NONE', #90778 ) ;
#82658=EDGE_CURVE ( 'NONE', #44279, #23445, #135007, .T. ) ;
#82659=CARTESIAN_POINT ( 'NONE',  ( -66.18398860626901126, 28.73617430169833753, 5.000000000000000000 ) ) ;
#82661=FACE_BOUND ( 'NONE', #113941, .T. ) ;
#82662=ORIENTED_EDGE ( 'NONE', *, *, #23589, .F. ) ;
#82663=PLANE ( 'NONE',  #143061 ) ;
#82664=LINE ( 'NONE', #50743, #29546 ) ;
#82665=LINE ( 'NONE', #5774, #139478 ) ;
#82666=ORIENTED_EDGE ( 'NONE', *, *, #126023, .F. ) ;
#82667=DIRECTION ( 'NONE',  ( 0.7071067811865487940, -0.7071067811865463515, 0.000000000000000000 ) ) ;
#82668=ORIENTED_EDGE ( 'NONE', *, *, #54228, .T. ) ;
#82669=VERTEX_POINT ( 'NONE', #84198 ) ;
#82670=VECTOR ( 'NONE', #130807, 1000.000000000000000 ) ;
#82671=VERTEX_POINT ( 'NONE', #105193 ) ;
#82672=VECTOR ( 'NONE', #88531, 1000.000000000000227 ) ;
#82673=AXIS2_PLACEMENT_3D ( 'NONE', #36074, #102026, #78868 ) ;
#82675=ORIENTED_EDGE ( 'NONE', *, *, #57015, .T. ) ;
#82678=EDGE_CURVE ( 'NONE', #47759, #9906, #72624, .T. ) ;
#82679=AXIS2_PLACEMENT_3D ( 'NONE', #130397, #85425, #98463 ) ;
#82680=DIRECTION ( 'NONE',  ( 0.7071067811865487940, 0.7071067811865463515, 0.000000000000000000 ) ) ;
#82681=AXIS2_PLACEMENT_3D ( 'NONE', #37140, #37882, #79269 ) ;
#82682=CARTESIAN_POINT ( 'NONE',  ( -30.48921356237309510, -27.52281430457076894, 5.000000000000000000 ) ) ;
#82683=PLANE ( 'NONE',  #80740 ) ;
#82684=LINE ( 'NONE', #3636, #48637 ) ;
#82685=CARTESIAN_POINT ( 'NONE',  ( 3.489213562373097322, -27.52281430457057709, 5.000000000000000000 ) ) ;
#82687=LINE ( 'NONE', #39175, #132750 ) ;
#82688=ORIENTED_EDGE ( 'NONE', *, *, #106172, .T. ) ;
#82689=ORIENTED_EDGE ( 'NONE', *, *, #130980, .F. ) ;
#82691=ORIENTED_EDGE ( 'NONE', *, *, #47642, .T. ) ;
#82693=ORIENTED_EDGE ( 'NONE', *, *, #57389, .T. ) ;
#82694=ORIENTED_EDGE ( 'NONE', *, *, #79535, .F. ) ;
#82695=DIRECTION ( 'NONE',  ( 1.000000000000000000, -0.000000000000000000, -0.000000000000000000 ) ) ;
#82697=ADVANCED_FACE ( 'NONE', ( #116784 ), #48685, .F. ) ;
#82698=DIRECTION ( 'NONE',  ( -0.000000000000000000, 0.3543493200069153248, 0.9351131265310292928 ) ) ;
#82699=VERTEX_POINT ( 'NONE', #73303 ) ;
#82700=AXIS2_PLACEMENT_3D ( 'NONE', #124403, #71457, #104786 ) ;
#82704=PLANE ( 'NONE',  #51955 ) ;
#82707=ORIENTED_EDGE ( 'NONE', *, *, #20789, .F. ) ;
#82709=PLANE ( 'NONE',  #142509 ) ;
#82712=ORIENTED_EDGE ( 'NONE', *, *, #24998, .F. ) ;
#82713=ORIENTED_EDGE ( 'NONE', *, *, #77730, .T. ) ;
#82714=CARTESIAN_POINT ( 'NONE',  ( 3.278254515685707027, 8.259292476615637923, 11.78515199841151073 ) ) ;
#82715=EDGE_LOOP ( 'NONE', ( #83982, #97213, #23906, #70231 ) ) ;
#82716=CARTESIAN_POINT ( 'NONE',  ( -21.49816348513943609, -17.24070752338411339, 8.407044977365272231 ) ) ;
#82717=CARTESIAN_POINT ( 'NONE',  ( 0.4232784580635307048, 11.25929247661560240, 17.85071094206584519 ) ) ;
#82718=FACE_OUTER_BOUND ( 'NONE', #132245, .T. ) ;
#82719=LINE ( 'NONE', #126899, #97944 ) ;
#82721=ORIENTED_EDGE ( 'NONE', *, *, #16717, .F. ) ;
#82722=EDGE_CURVE ( 'NONE', #118694, #108262, #37826, .T. ) ;
#82723=DIRECTION ( 'NONE',  ( -0.6830127018922180770, -0.6830127018922204085, -0.2588190451025213501 ) ) ;
#82724=ADVANCED_FACE ( 'NONE', ( #117473 ), #127682, .T. ) ;
#82725=CARTESIAN_POINT ( 'NONE',  ( 48.48921356237309510, -27.52281430457089328, 5.000000000000000000 ) ) ;
#82726=DIRECTION ( 'NONE',  ( -0.000000000000000000, -0.3543493200069152693, 0.9351131265310292928 ) ) ;
#82728=ORIENTED_EDGE ( 'NONE', *, *, #72900, .F. ) ;
#82729=PLANE ( 'NONE',  #111464 ) ;
#82730=FACE_OUTER_BOUND ( 'NONE', #36393, .T. ) ;
#82731=ORIENTED_EDGE ( 'NONE', *, *, #126643, .T. ) ;
#82732=FACE_OUTER_BOUND ( 'NONE', #54201, .T. ) ;
#82733=EDGE_LOOP ( 'NONE', ( #81500, #75261, #68780, #12985 ) ) ;
#82734=EDGE_CURVE ( 'NONE', #95876, #137275, #128392, .T. ) ;
#82735=ORIENTED_EDGE ( 'NONE', *, *, #7792, .F. ) ;
#82738=ORIENTED_EDGE ( 'NONE', *, *, #102975, .T. ) ;
#82739=DIRECTION ( 'NONE',  ( 2.781805975412905274E-17, -0.3543493200069152138, 0.9351131265310292928 ) ) ;
#82740=LINE ( 'NONE', #61717, #142382 ) ;
#82741=CARTESIAN_POINT ( 'NONE',  ( -34.47516574401893052, 18.02806734111563358, 4.998110765256835286 ) ) ;
#82742=VECTOR ( 'NONE', #140752, 999.9999999999998863 ) ;
#82744=ORIENTED_EDGE ( 'NONE', *, *, #75394, .F. ) ;
#82745=PLANE ( 'NONE',  #143416 ) ;
#82746=CARTESIAN_POINT ( 'NONE',  ( -33.70701326429281153, -21.74070752338405299, 4.999753212805220670 ) ) ;
#82747=LINE ( 'NONE', #12649, #74256 ) ;
#82750=LINE ( 'NONE', #127686, #25786 ) ;
#82751=LINE ( 'NONE', #137128, #140923 ) ;
#82753=DIRECTION ( 'NONE',  ( -0.7071067811865486830, 0.7071067811865464625, 0.000000000000000000 ) ) ;
#82754=ORIENTED_EDGE ( 'NONE', *, *, #34397, .T. ) ;
#82755=EDGE_LOOP ( 'NONE', ( #33296, #101605, #58265, #19176 ) ) ;
#82756=VERTEX_POINT ( 'NONE', #105881 ) ;
#82758=VECTOR ( 'NONE', #25691, 1000.000000000000000 ) ;
#82759=EDGE_LOOP ( 'NONE', ( #137096, #131224, #10514, #49550 ) ) ;
#82760=EDGE_CURVE ( 'NONE', #3592, #128295, #16758, .T. ) ;
#82761=ORIENTED_EDGE ( 'NONE', *, *, #77644, .T. ) ;
#82763=CARTESIAN_POINT ( 'NONE',  ( -24.18398860626899705, 28.73617430169804265, 5.000000000000000000 ) ) ;
#82764=CARTESIAN_POINT ( 'NONE',  ( 29.20710678118634718, -17.24070752338410628, 5.000000000000000000 ) ) ;
#82766=LINE ( 'NONE', #29090, #76374 ) ;
#82767=CARTESIAN_POINT ( 'NONE',  ( -34.92500000000001137, 21.66246187583877258, 4.000000000000000000 ) ) ;
#82768=AXIS2_PLACEMENT_3D ( 'NONE', #50543, #94732, #138995 ) ;
#82769=DIRECTION ( 'NONE',  ( 0.7071067811865487940, 0.7071067811865463515, 0.000000000000000000 ) ) ;
#82770=DIRECTION ( 'NONE',  ( 0.6830127018922180770, -0.6830127018922204085, -0.2588190451025213501 ) ) ;
#82773=ADVANCED_FACE ( 'NONE', ( #114632 ), #27625, .F. ) ;
#82775=DIRECTION ( 'NONE',  ( -0.6830127018922180770, -0.6830127018922204085, -0.2588190451025214056 ) ) ;
#82776=DIRECTION ( 'NONE',  ( -0.000000000000000000, 0.3543493200069153248, 0.9351131265310292928 ) ) ;
#82778=DIRECTION ( 'NONE',  ( -0.000000000000000000, 0.3543493200069153248, 0.9351131265310292928 ) ) ;
#82780=DIRECTION ( 'NONE',  ( -0.7071067811865487940, 0.7071067811865463515, -0.000000000000000000 ) ) ;
#82781=PLANE ( 'NONE',  #19943 ) ;
#82782=VECTOR ( 'NONE', #105779, 1000.000000000000227 ) ;
#82784=LINE ( 'NONE', #71205, #99950 ) ;
#82785=EDGE_CURVE ( 'NONE', #51759, #4075, #95746, .T. ) ;
#82786=VECTOR ( 'NONE', #16050, 1000.000000000000000 ) ;
#82787=EDGE_CURVE ( 'NONE', #4323, #24129, #116063, .T. ) ;
#82788=CARTESIAN_POINT ( 'NONE',  ( -42.29974487139158157, -27.71228299555235708, 4.000000000000000000 ) ) ;
#82789=ORIENTED_EDGE ( 'NONE', *, *, #56208, .T. ) ;
#82790=ORIENTED_EDGE ( 'NONE', *, *, #111232, .T. ) ;
#82794=LINE ( 'NONE', #116103, #104170 ) ;
#82795=EDGE_CURVE ( 'NONE', #91137, #51968, #59581, .T. ) ;
#82796=LINE ( 'NONE', #4425, #71041 ) ;
#82797=VECTOR ( 'NONE', #70871, 1000.000000000000000 ) ;
#82798=ORIENTED_EDGE ( 'NONE', *, *, #80293, .F. ) ;
#82799=EDGE_CURVE ( 'NONE', #80231, #57697, #105465, .T. ) ;
#82800=CARTESIAN_POINT ( 'NONE',  ( -18.18398860626898994, 28.73617430169800002, 5.000000000000000000 ) ) ;
#82801=DIRECTION ( 'NONE',  ( 0.7071067811865487940, 0.7071067811865463515, 0.000000000000000000 ) ) ;
#82802=CARTESIAN_POINT ( 'NONE',  ( 18.18398860626898994, 28.73617430169800002, 5.000000000000000000 ) ) ;
#82803=LINE ( 'NONE', #95068, #41874 ) ;
#82804=EDGE_CURVE ( 'NONE', #107216, #109623, #62429, .T. ) ;
#82806=ORIENTED_EDGE ( 'NONE', *, *, #25662, .F. ) ;
#82807=EDGE_CURVE ( 'NONE', #8819, #115197, #94315, .T. ) ;
#82808=LINE ( 'NONE', #17515, #15471 ) ;
#82809=VERTEX_POINT ( 'NONE', #61721 ) ;
#82810=CARTESIAN_POINT ( 'NONE',  ( -7.001930566820925961, -22.22500000000000142, 4.500000000000000888 ) ) ;
#82812=LINE ( 'NONE', #126993, #123128 ) ;
#82815=ORIENTED_EDGE ( 'NONE', *, *, #56875, .T. ) ;
#82819=CARTESIAN_POINT ( 'NONE',  ( 0.2997448713915885632, -27.71228299555206220, 4.000000000000000000 ) ) ;
#82821=CARTESIAN_POINT ( 'NONE',  ( 17.99999999999987210, -4.068876922607775448, 4.000000000000000000 ) ) ;
#82822=AXIS2_PLACEMENT_3D ( 'NONE', #76468, #55419, #20618 ) ;
#82824=( BOUNDED_CURVE ( )  B_SPLINE_CURVE ( 3, ( #62966, #42644, #17963, #8503 ),
 .UNSPECIFIED., .F., .T. ) 
 B_SPLINE_CURVE_WITH_KNOTS ( ( 4, 4 ),
 ( 1.964434688349490754, 3.503810798801452187 ),
 .UNSPECIFIED. ) 
 CURVE ( )  GEOMETRIC_REPRESENTATION_ITEM ( )  RATIONAL_B_SPLINE_CURVE ( ( 1.000000000000000000, 0.8120851936182287290, 0.8120851936182287290, 1.000000000000000000 ) ) 
 REPRESENTATION_ITEM ( '' )  );
#82825=EDGE_CURVE ( 'NONE', #54370, #93386, #63157, .T. ) ;
#82826=VECTOR ( 'NONE', #63669, 1000.000000000000000 ) ;
#82828=ORIENTED_EDGE ( 'NONE', *, *, #95195, .T. ) ;
#82829=CARTESIAN_POINT ( 'NONE',  ( 4.499999999999967137, 12.05218569542904561, 5.000000000000000000 ) ) ;
#82830=CARTESIAN_POINT ( 'NONE',  ( 5.207106781186507050, -5.240707523384232402, 5.000000000000000000 ) ) ;
#82831=ORIENTED_EDGE ( 'NONE', *, *, #44329, .F. ) ;
#82832=ORIENTED_EDGE ( 'NONE', *, *, #40297, .T. ) ;
#82833=CARTESIAN_POINT ( 'NONE',  ( -5.207106781186507050, 3.759292476615680112, 5.000000000000000000 ) ) ;
#82834=EDGE_LOOP ( 'NONE', ( #109571, #35968, #130317, #34620, #62788, #78537, #134265, #87895, #32663, #63763, #82326, #15247, #139, #13205, #90693, #58256, #95102, #19891, #109378, #30135, #27452, #89613, #62019, #63602, #67837, #30547, #139561, #118393, #69479, #93721, #126599, #104502, #139016, #28919, #60687, #143037, #85352, #28740, #133511, #139732, #16489, #30560, #142456, #43385 ) ) ;
#82835=DIRECTION ( 'NONE',  ( -0.7071067811865487940, 0.7071067811865463515, -0.000000000000000000 ) ) ;
#82836=VERTEX_POINT ( 'NONE', #84873 ) ;
#82837=DIRECTION ( 'NONE',  ( -0.7071067811865486830, -0.7071067811865464625, 0.000000000000000000 ) ) ;
#82838=EDGE_CURVE ( 'NONE', #57316, #135321, #6355, .T. ) ;
#82841=FACE_BOUND ( 'NONE', #208, .T. ) ;
#82843=LINE ( 'NONE', #37177, #140536 ) ;
#82844=ORIENTED_EDGE ( 'NONE', *, *, #93518, .F. ) ;
#82845=CARTESIAN_POINT ( 'NONE',  ( -13.43359823057990354, 1.153863645259229909, 4.000000000000000000 ) ) ;
#82846=CARTESIAN_POINT ( 'NONE',  ( -10.49999999999992539, 6.277155672890260441, -3.510561720658917473 ) ) ;
#82848=VERTEX_POINT ( 'NONE', #86319 ) ;
#82849=FACE_OUTER_BOUND ( 'NONE', #44393, .T. ) ;
#82850=EDGE_CURVE ( 'NONE', #98330, #63466, #142136, .T. ) ;
#82851=VERTEX_POINT ( 'NONE', #119610 ) ;
#82852=EDGE_LOOP ( 'NONE', ( #51170, #107602, #131463, #37472 ) ) ;
#82854=ORIENTED_EDGE ( 'NONE', *, *, #80238, .T. ) ;
#82857=CARTESIAN_POINT ( 'NONE',  ( -60.18398860626900415, 28.73617430169829490, 5.000000000000000000 ) ) ;
#82859=VERTEX_POINT ( 'NONE', #131234 ) ;
#82862=CARTESIAN_POINT ( 'NONE',  ( 27.32816939922334143, -6.740707523384214639, 4.000000000000000000 ) ) ;
#82863=ADVANCED_FACE ( 'NONE', ( #31925 ), #21028, .F. ) ;
#82864=CARTESIAN_POINT ( 'NONE',  ( 57.29974487139158157, -27.71228299555246011, 4.000000000000000000 ) ) ;
#82865=PLANE ( 'NONE',  #119873 ) ;
#82867=LINE ( 'NONE', #84986, #99481 ) ;
#82868=ORIENTED_EDGE ( 'NONE', *, *, #13415, .T. ) ;
#82869=ORIENTED_EDGE ( 'NONE', *, *, #72832, .F. ) ;
#82870=CARTESIAN_POINT ( 'NONE',  ( 14.11732500641695509, -0.1862019290248694003, 4.000000000000000000 ) ) ;
#82871=AXIS2_PLACEMENT_3D ( 'NONE', #128008, #38837, #104798 ) ;
#82872=PLANE ( 'NONE',  #7253 ) ;
#82873=VERTEX_POINT ( 'NONE', #66010 ) ;
#82875=VECTOR ( 'NONE', #10411, 1000.000000000000000 ) ;
#82876=ORIENTED_EDGE ( 'NONE', *, *, #139482, .F. ) ;
#82877=LINE ( 'NONE', #72754, #130072 ) ;
#82878=EDGE_CURVE ( 'NONE', #104684, #99346, #110174, .T. ) ;
#82880=ORIENTED_EDGE ( 'NONE', *, *, #119086, .F. ) ;
#82881=CARTESIAN_POINT ( 'NONE',  ( -2.229957205422064437, 21.73644205237997440, 5.000000000000000888 ) ) ;
#82886=DIRECTION ( 'NONE',  ( -0.7071067811865486830, -0.7071067811865464625, -0.000000000000000000 ) ) ;
#82887=EDGE_LOOP ( 'NONE', ( #66381, #107761, #27293, #43178, #1124, #84500 ) ) ;
#82888=DIRECTION ( 'NONE',  ( -0.000000000000000000, 0.000000000000000000, 1.000000000000000000 ) ) ;
#82890=DIRECTION ( 'NONE',  ( -0.000000000000000000, 0.000000000000000000, 1.000000000000000000 ) ) ;
#82891=CARTESIAN_POINT ( 'NONE',  ( -29.99999999999978328, 14.96639925780210767, 5.000000000000000000 ) ) ;
#82892=ORIENTED_EDGE ( 'NONE', *, *, #129200, .F. ) ;
#82894=VERTEX_POINT ( 'NONE', #33394 ) ;
#82895=DIRECTION ( 'NONE',  ( 0.7071067811865487940, 0.7071067811865463515, 0.000000000000000000 ) ) ;
#82896=LINE ( 'NONE', #37233, #81612 ) ;
#82897=ADVANCED_FACE ( 'NONE', ( #57997 ), #46414, .F. ) ;
#82898=FACE_OUTER_BOUND ( 'NONE', #101640, .T. ) ;
#82899=EDGE_LOOP ( 'NONE', ( #58090, #117865, #71994, #65961 ) ) ;
#82900=ADVANCED_FACE ( 'NONE', ( #102191 ), #35534, .F. ) ;
#82901=CARTESIAN_POINT ( 'NONE',  ( 30.70710678118632231, -15.74070752338412760, 5.000000000000000000 ) ) ;
#82903=CYLINDRICAL_SURFACE ( 'NONE', #51358, 0.5000000000000004441 ) ;
#82905=CARTESIAN_POINT ( 'NONE',  ( 10.17183060077640633, -2.240707523384257716, 4.000000000000000000 ) ) ;
#82906=LINE ( 'NONE', #60458, #121041 ) ;
#82911=EDGE_LOOP ( 'NONE', ( #58167, #90267, #117218, #24356 ) ) ;
#82912=EDGE_CURVE ( 'NONE', #119060, #63022, #13705, .T. ) ;
#82913=EDGE_LOOP ( 'NONE', ( #121239, #128381, #87631, #133153 ) ) ;
#82915=CARTESIAN_POINT ( 'NONE',  ( 17.99999999999987566, -4.447814304570784749, 5.000000000000000000 ) ) ;
#82916=PLANE ( 'NONE',  #140912 ) ;
#82919=DIRECTION ( 'NONE',  ( -0.7071067811865486830, -0.7071067811865464625, 0.000000000000000000 ) ) ;
#82921=DIRECTION ( 'NONE',  ( -0.000000000000000000, 0.3543493200069153248, 0.9351131265310292928 ) ) ;
#82922=LINE ( 'NONE', #37998, #53770 ) ;
#82924=DIRECTION ( 'NONE',  ( 0.6830127018922180770, -0.6830127018922204085, -0.2588190451025213501 ) ) ;
#82925=CARTESIAN_POINT ( 'NONE',  ( -8.999999999999937828, -1.068876922607800761, 4.000000000000000000 ) ) ;
#82926=CARTESIAN_POINT ( 'NONE',  ( -16.49999999999988276, -10.91253812416064228, 4.000000000000000000 ) ) ;
#82928=ADVANCED_FACE ( 'NONE', ( #11559 ), #143535, .F. ) ;
#82931=ORIENTED_EDGE ( 'NONE', *, *, #130768, .T. ) ;
#82933=CARTESIAN_POINT ( 'NONE',  ( -28.49999999999980105, -5.947814304570768762, 5.000000000000000000 ) ) ;
#82934=CARTESIAN_POINT ( 'NONE',  ( -5.999999999999950262, -4.447814304570779420, 5.000000000000000000 ) ) ;
#82935=FACE_OUTER_BOUND ( 'NONE', #68608, .T. ) ;
#82937=DIRECTION ( 'NONE',  ( -0.7071067811865486830, -0.7071067811865464625, 0.000000000000000000 ) ) ;
#82938=ORIENTED_EDGE ( 'NONE', *, *, #101936, .T. ) ;
#82940=LINE ( 'NONE', #127135, #14439 ) ;
#82941=DIRECTION ( 'NONE',  ( -0.6830127018922181881, 0.6830127018922202975, -0.2588190451025214056 ) ) ;
#82942=DIRECTION ( 'NONE',  ( -0.6830127018922180770, -0.6830127018922204085, -0.2588190451025213501 ) ) ;
#82945=ADVANCED_FACE ( 'NONE', ( #23914 ), #121763, .T. ) ;
#82946=CARTESIAN_POINT ( 'NONE',  ( 45.48921356237309510, -27.52281430457087197, 5.000000000000000000 ) ) ;
#82947=EDGE_LOOP ( 'NONE', ( #135714, #87037, #132928, #47899 ) ) ;
#82948=VERTEX_POINT ( 'NONE', #22441 ) ;
#82949=VECTOR ( 'NONE', #40093, 1000.000000000000000 ) ;
#82951=DIRECTION ( 'NONE',  ( -0.7071067811865486830, -0.7071067811865464625, -0.000000000000000000 ) ) ;
#82952=ADVANCED_FACE ( 'NONE', ( #123948 ), #79766, .F. ) ;
#82953=CARTESIAN_POINT ( 'NONE',  ( -15.48921356237309510, -27.52281430457066236, 5.000000000000000000 ) ) ;
#82955=EDGE_LOOP ( 'NONE', ( #131078, #83357, #101984, #49533 ) ) ;
#82956=EDGE_CURVE ( 'NONE', #28313, #36187, #122479, .T. ) ;
#82958=VECTOR ( 'NONE', #18122, 1000.000000000000000 ) ;
#82959=LINE ( 'NONE', #72117, #111477 ) ;
#82961=CARTESIAN_POINT ( 'NONE',  ( 21.48921356237309155, -27.52281430457070499, 5.000000000000000000 ) ) ;
#82962=EDGE_LOOP ( 'NONE', ( #116767, #130062, #134218, #102588 ) ) ;
#82963=ORIENTED_EDGE ( 'NONE', *, *, #63030, .F. ) ;
#82964=DIRECTION ( 'NONE',  ( 0.7071067811865487940, -0.7071067811865463515, 0.000000000000000000 ) ) ;
#82965=AXIS2_PLACEMENT_3D ( 'NONE', #57960, #126048, #67395 ) ;
#82966=LINE ( 'NONE', #19126, #15258 ) ;
#82967=CARTESIAN_POINT ( 'NONE',  ( 48.18398860626899705, 28.73617430169820608, 5.000000000000000000 ) ) ;
#82968=AXIS2_PLACEMENT_3D ( 'NONE', #80172, #46860, #103301 ) ;
#82969=EDGE_CURVE ( 'NONE', #86438, #25446, #66700, .T. ) ;
#82970=CARTESIAN_POINT ( 'NONE',  ( -42.18398860626899705, 28.73617430169816700, 5.000000000000000000 ) ) ;
#82971=EDGE_CURVE ( 'NONE', #54208, #5533, #88463, .T. ) ;
#82972=DIRECTION ( 'NONE',  ( 0.7071067811865487940, 0.7071067811865463515, -0.000000000000000000 ) ) ;
#82973=CARTESIAN_POINT ( 'NONE',  ( 36.29974487139159578, -27.71228299555231445, 4.000000000000000000 ) ) ;
#82974=EDGE_LOOP ( 'NONE', ( #94325, #34756, #11026, #45103 ) ) ;
#82975=DIRECTION ( 'NONE',  ( -0.000000000000000000, 0.3543493200069153248, 0.9351131265310292928 ) ) ;
#82976=DIRECTION ( 'NONE',  ( 0.6830127018922181881, 0.6830127018922202975, -0.2588190451025214056 ) ) ;
#82977=CARTESIAN_POINT ( 'NONE',  ( 24.18398860626899705, 28.73617430169804265, 5.000000000000000000 ) ) ;
#82978=VECTOR ( 'NONE', #98538, 999.9999999999998863 ) ;
#82979=PLANE ( 'NONE',  #96981 ) ;
#82980=VECTOR ( 'NONE', #87651, 1000.000000000000000 ) ;
#82981=ADVANCED_FACE ( 'NONE', ( #110873 ), #135536, .F. ) ;
#82982=EDGE_LOOP ( 'NONE', ( #106860, #136668, #52277, #47595 ) ) ;
#82987=CARTESIAN_POINT ( 'NONE',  ( -34.92500000000001137, 1.701930566820992308, 4.500000000000000888 ) ) ;
#82988=EDGE_LOOP ( 'NONE', ( #93130, #4801, #16827, #48816 ) ) ;
#82990=ADVANCED_FACE ( 'NONE', ( #25312 ), #44994, .F. ) ;
#82991=VECTOR ( 'NONE', #107496, 1000.000000000000000 ) ;
#82992=CARTESIAN_POINT ( 'NONE',  ( -27.18398860626900060, 28.73617430169806042, 5.000000000000000000 ) ) ;
#82994=VERTEX_POINT ( 'NONE', #124638 ) ;
#82995=ORIENTED_EDGE ( 'NONE', *, *, #43942, .F. ) ;
#82996=VECTOR ( 'NONE', #102900, 1000.000000000000000 ) ;
#82997=CARTESIAN_POINT ( 'NONE',  ( -45.18398860626900415, 28.73617430169818832, 5.000000000000000000 ) ) ;
#82998=ORIENTED_EDGE ( 'NONE', *, *, #109477, .F. ) ;
#83000=EDGE_CURVE ( 'NONE', #8977, #77966, #115601, .T. ) ;
#83001=CARTESIAN_POINT ( 'NONE',  ( -0.2997448713915885632, -27.71228299555206220, 4.000000000000000000 ) ) ;
#83002=AXIS2_PLACEMENT_3D ( 'NONE', #8689, #63863, #52938 ) ;
#83005=FACE_BOUND ( 'NONE', #112331, .T. ) ;
#83007=DIRECTION ( 'NONE',  ( -0.7071067811865486830, -0.7071067811865464625, 0.000000000000000000 ) ) ;
#83008=VERTEX_POINT ( 'NONE', #89168 ) ;
#83011=ADVANCED_FACE ( 'NONE', ( #13002 ), #101452, .F. ) ;
#83015=VERTEX_POINT ( 'NONE', #30137 ) ;
#83017=CARTESIAN_POINT ( 'NONE',  ( 13.49999999999991118, 9.052185695429077583, 5.000000000000000000 ) ) ;
#83018=( BOUNDED_CURVE ( )  B_SPLINE_CURVE ( 3, ( #7555, #40928, #51815, #130080 ),
 .UNSPECIFIED., .F., .F. ) 
 B_SPLINE_CURVE_WITH_KNOTS ( ( 4, 4 ),
 ( 5.920967161967928050, 7.341195215986656031 ),
 .UNSPECIFIED. ) 
 CURVE ( )  GEOMETRIC_REPRESENTATION_ITEM ( )  RATIONAL_B_SPLINE_CURVE ( ( 1.000000000000000000, 0.8388583629366577199, 0.8388583629366577199, 1.000000000000000000 ) ) 
 REPRESENTATION_ITEM ( '' )  );
#83019=DIRECTION ( 'NONE',  ( -0.000000000000000000, 0.000000000000000000, 1.000000000000000000 ) ) ;
#83021=DIRECTION ( 'NONE',  ( 0.3543493200069163240, 0.000000000000000000, -0.9351131265310288487 ) ) ;
#83022=ORIENTED_EDGE ( 'NONE', *, *, #76492, .F. ) ;
#83023=DIRECTION ( 'NONE',  ( 0.000000000000000000, -1.000000000000000000, -0.000000000000000000 ) ) ;
#83024=CARTESIAN_POINT ( 'NONE',  ( -10.49999999999993250, 10.08746187583914633, 4.000000000000000000 ) ) ;
#83025=ADVANCED_FACE ( 'NONE', ( #36906 ), #28012, .F. ) ;
#83026=DIRECTION ( 'NONE',  ( 1.000000000000000000, 0.000000000000000000, 0.000000000000000000 ) ) ;
#83027=DIRECTION ( 'NONE',  ( -0.000000000000000000, -0.3543493200069152693, 0.9351131265310292928 ) ) ;
#83028=FACE_OUTER_BOUND ( 'NONE', #110751, .T. ) ;
#83029=DIRECTION ( 'NONE',  ( 0.7071067811865487940, -0.7071067811865463515, 0.000000000000000000 ) ) ;
#83030=LINE ( 'NONE', #49711, #76996 ) ;
#83031=ORIENTED_EDGE ( 'NONE', *, *, #72131, .T. ) ;
#83032=CARTESIAN_POINT ( 'NONE',  ( 39.48921356237310221, -27.52281430457082934, 5.000000000000000000 ) ) ;
#83033=LINE ( 'NONE', #113492, #120571 ) ;
#83034=ORIENTED_EDGE ( 'NONE', *, *, #78185, .T. ) ;
#83036=EDGE_CURVE ( 'NONE', #96152, #49642, #138926, .T. ) ;
#83037=ORIENTED_EDGE ( 'NONE', *, *, #108637, .T. ) ;
#83039=ORIENTED_EDGE ( 'NONE', *, *, #89496, .T. ) ;
#83042=ORIENTED_EDGE ( 'NONE', *, *, #135008, .F. ) ;
#83043=DIRECTION ( 'NONE',  ( -0.7071067811865486830, -0.7071067811865464625, 0.000000000000000000 ) ) ;
#83045=CARTESIAN_POINT ( 'NONE',  ( 72.48921356237309510, -27.52281430457106026, 5.000000000000000000 ) ) ;
#83046=CARTESIAN_POINT ( 'NONE',  ( -23.51078643762690490, -27.52281430457038880, 5.000000000000000000 ) ) ;
#83047=CARTESIAN_POINT ( 'NONE',  ( -51.18398860626899705, 28.73617430169823095, 5.000000000000000000 ) ) ;
#83048=VERTEX_POINT ( 'NONE', #116449 ) ;
#83049=ORIENTED_EDGE ( 'NONE', *, *, #6436, .T. ) ;
#83051=CARTESIAN_POINT ( 'NONE',  ( 31.49999999999977973, -13.53360074219760101, 5.000000000000000000 ) ) ;
#83052=ORIENTED_EDGE ( 'NONE', *, *, #62945, .T. ) ;
#83053=CARTESIAN_POINT ( 'NONE',  ( 10.49999999999992895, 15.43112307739203182, 4.000000000000000000 ) ) ;
#83054=ORIENTED_EDGE ( 'NONE', *, *, #142994, .T. ) ;
#83055=EDGE_CURVE ( 'NONE', #124292, #142286, #117138, .T. ) ;
#83057=ORIENTED_EDGE ( 'NONE', *, *, #16642, .F. ) ;
#83058=VERTEX_POINT ( 'NONE', #17817 ) ;
#83059=LINE ( 'NONE', #51875, #42476 ) ;
#83061=VECTOR ( 'NONE', #107818, 1000.000000000000227 ) ;
#83064=AXIS2_PLACEMENT_3D ( 'NONE', #4291, #85476, #28273 ) ;
#83065=LINE ( 'NONE', #6879, #10014 ) ;
#83066=EDGE_CURVE ( 'NONE', #130315, #65177, #83107, .T. ) ;
#83067=CARTESIAN_POINT ( 'NONE',  ( 3.005480084712505828, 28.92564299267936079, 4.000000000000000000 ) ) ;
#83069=EDGE_CURVE ( 'NONE', #84409, #4761, #73661, .T. ) ;
#83070=DIRECTION ( 'NONE',  ( 0.6830127018922181881, 0.6830127018922202975, -0.2588190451025214056 ) ) ;
#83076=CARTESIAN_POINT ( 'NONE',  ( 20.99999999999985434, -7.068876922607736368, 4.000000000000000000 ) ) ;
#83077=LINE ( 'NONE', #72954, #6629 ) ;
#83078=CARTESIAN_POINT ( 'NONE',  ( 53.99451991528749062, 28.92564299267975869, 4.000000000000000000 ) ) ;
#83081=ORIENTED_EDGE ( 'NONE', *, *, #13560, .F. ) ;
#83082=LINE ( 'NONE', #7634, #134336 ) ;
#83084=DIRECTION ( 'NONE',  ( 0.3543493200069162685, -0.000000000000000000, -0.9351131265310288487 ) ) ;
#83085=PLANE ( 'NONE',  #133083 ) ;
#83088=EDGE_CURVE ( 'NONE', #44162, #129671, #29422, .T. ) ;
#83090=VECTOR ( 'NONE', #34441, 1000.000000000000000 ) ;
#83091=LINE ( 'NONE', #4746, #117828 ) ;
#83092=CARTESIAN_POINT ( 'NONE',  ( 66.18398860626901126, 28.73617430169833753, 5.000000000000000000 ) ) ;
#83093=LINE ( 'NONE', #8341, #104331 ) ;
#83094=PLANE ( 'NONE',  #134 ) ;
#83097=DIRECTION ( 'NONE',  ( -0.7071067811865486830, -0.7071067811865464625, 0.000000000000000000 ) ) ;
#83098=ORIENTED_EDGE ( 'NONE', *, *, #94110, .T. ) ;
#83099=VECTOR ( 'NONE', #107017, 1000.000000000000000 ) ;
#83100=DIRECTION ( 'NONE',  ( -0.3543493200069162685, -0.000000000000000000, -0.9351131265310288487 ) ) ;
#83101=CARTESIAN_POINT ( 'NONE',  ( 25.56687199751241835, -21.74070752338406365, 6.915939825044013389 ) ) ;
#83102=VERTEX_POINT ( 'NONE', #102901 ) ;
#83103=CARTESIAN_POINT ( 'NONE',  ( 22.36246187583885359, 22.22500000000000853, 4.000000000000000000 ) ) ;
#83104=CARTESIAN_POINT ( 'NONE',  ( -18.79333936457834753, 21.75929247661549937, 4.998822639870701856 ) ) ;
#83105=VERTEX_POINT ( 'NONE', #61400 ) ;
#83107=LINE ( 'NONE', #6919, #116088 ) ;
#83108=CARTESIAN_POINT ( 'NONE',  ( 0.000000000000000000, 0.000000000000000000, 5.000000000000000000 ) ) ;
#83111=AXIS2_PLACEMENT_3D ( 'NONE', #42031, #31854, #108654 ) ;
#83115=EDGE_CURVE ( 'NONE', #63249, #92319, #3540, .T. ) ;
#83118=CARTESIAN_POINT ( 'NONE',  ( -13.49999999999989342, -17.94781430457065241, 5.000000000000000000 ) ) ;
#83120=CARTESIAN_POINT ( 'NONE',  ( -44.99451991528749772, 28.92564299267969474, 4.000000000000000000 ) ) ;
#83122=LINE ( 'NONE', #127322, #127851 ) ;
#83124=CARTESIAN_POINT ( 'NONE',  ( -8.994519915287490619, 28.92564299267944250, 4.000000000000000000 ) ) ;
#83125=ORIENTED_EDGE ( 'NONE', *, *, #83036, .F. ) ;
#83126=EDGE_CURVE ( 'NONE', #66379, #80080, #118577, .T. ) ;
#83127=ADVANCED_FACE ( 'NONE', ( #28741 ), #51920, .F. ) ;
#83129=ORIENTED_EDGE ( 'NONE', *, *, #69548, .T. ) ;
#83131=PLANE ( 'NONE',  #105557 ) ;
#83132=DIRECTION ( 'NONE',  ( 0.3543493200069162685, -0.000000000000000000, -0.9351131265310288487 ) ) ;
#83133=DIRECTION ( 'NONE',  ( 0.6830127018922180770, -0.6830127018922204085, -0.2588190451025213501 ) ) ;
#83134=ORIENTED_EDGE ( 'NONE', *, *, #52806, .T. ) ;
#83135=LINE ( 'NONE', #71553, #48868 ) ;
#83136=DIRECTION ( 'NONE',  ( 0.000000000000000000, 1.000000000000000000, 0.000000000000000000 ) ) ;
#83138=LINE ( 'NONE', #7693, #62507 ) ;
#83139=EDGE_CURVE ( 'NONE', #18398, #59514, #133752, .T. ) ;
#83140=PLANE ( 'NONE',  #28581 ) ;
#83141=LINE ( 'NONE', #40374, #140090 ) ;
#83143=FACE_OUTER_BOUND ( 'NONE', #136703, .T. ) ;
#83144=CARTESIAN_POINT ( 'NONE',  ( -34.49999999999976552, 3.054329344830908344, 4.994342998332172101 ) ) ;
#83145=DIRECTION ( 'NONE',  ( 0.3543493200069162685, -0.000000000000000000, -0.9351131265310288487 ) ) ;
#83146=CARTESIAN_POINT ( 'NONE',  ( 7.045157733366620434, -21.74070752338405654, 21.72585301388586032 ) ) ;
#83147=ORIENTED_EDGE ( 'NONE', *, *, #35686, .T. ) ;
#83148=ORIENTED_EDGE ( 'NONE', *, *, #115474, .T. ) ;
#83150=ORIENTED_EDGE ( 'NONE', *, *, #50552, .T. ) ;
#83151=EDGE_CURVE ( 'NONE', #139559, #125103, #42488, .T. ) ;
#83152=CARTESIAN_POINT ( 'NONE',  ( -34.92500000000001137, 22.22500000000000142, 4.000000000000000000 ) ) ;
#83153=DIRECTION ( 'NONE',  ( 0.7071067811865487940, 0.7071067811865463515, 0.000000000000000000 ) ) ;
#83154=DIRECTION ( 'NONE',  ( -0.7071067811865486830, -0.7071067811865464625, 0.000000000000000000 ) ) ;
#83156=ADVANCED_FACE ( 'NONE', ( #88836 ), #21422, .F. ) ;
#83158=CARTESIAN_POINT ( 'NONE',  ( 39.29974487139159578, -27.71228299555233576, 4.000000000000000000 ) ) ;
#83160=AXIS2_PLACEMENT_3D ( 'NONE', #75416, #64525, #96406 ) ;
#83162=CARTESIAN_POINT ( 'NONE',  ( -11.51078643762690490, -27.52281430457047406, 5.000000000000000000 ) ) ;
#83163=EDGE_CURVE ( 'NONE', #86472, #106936, #87399, .T. ) ;
#83164=DIRECTION ( 'NONE',  ( 0.7071067811865486830, -0.7071067811865464625, -0.000000000000000000 ) ) ;
#83165=VECTOR ( 'NONE', #66449, 1000.000000000000000 ) ;
#83166=VECTOR ( 'NONE', #112430, 1000.000000000000114 ) ;
#83167=VECTOR ( 'NONE', #22838, 1000.000000000000000 ) ;
#83168=ORIENTED_EDGE ( 'NONE', *, *, #101230, .T. ) ;
#83169=ORIENTED_EDGE ( 'NONE', *, *, #91118, .F. ) ;
#83170=AXIS2_PLACEMENT_3D ( 'NONE', #59333, #2762, #101365 ) ;
#83171=DIRECTION ( 'NONE',  ( 0.6830127018922181881, 0.6830127018922202975, -0.2588190451025214056 ) ) ;
#83172=DIRECTION ( 'NONE',  ( 0.7071067811865487940, 0.7071067811865463515, 0.000000000000000000 ) ) ;
#83176=EDGE_CURVE ( 'NONE', #122031, #77426, #97536, .T. ) ;
#83178=CARTESIAN_POINT ( 'NONE',  ( -28.49999999999980460, -19.91253812416055169, 4.000000000000000000 ) ) ;
#83180=EDGE_CURVE ( 'NONE', #11459, #136204, #9056, .T. ) ;
#83181=EDGE_LOOP ( 'NONE', ( #77192, #77340, #88213, #136593 ) ) ;
#83182=ORIENTED_EDGE ( 'NONE', *, *, #86020, .T. ) ;
#83183=ORIENTED_EDGE ( 'NONE', *, *, #128655, .T. ) ;
#83184=VERTEX_POINT ( 'NONE', #67072 ) ;
#83186=VECTOR ( 'NONE', #20511, 999.9999999999998863 ) ;
#83187=LINE ( 'NONE', #115763, #75620 ) ;
#83189=ORIENTED_EDGE ( 'NONE', *, *, #128395, .T. ) ;
#83190=FACE_OUTER_BOUND ( 'NONE', #70014, .T. ) ;
#83192=CARTESIAN_POINT ( 'NONE',  ( 6.706123077391905163, 22.22500000000000142, 4.000000000000000000 ) ) ;
#83193=VECTOR ( 'NONE', #30574, 1000.000000000000227 ) ;
#83194=PLANE ( 'NONE',  #5106 ) ;
#83195=ORIENTED_EDGE ( 'NONE', *, *, #112910, .T. ) ;
#83196=VECTOR ( 'NONE', #140332, 1000.000000000000227 ) ;
#83197=DIRECTION ( 'NONE',  ( -0.000000000000000000, 0.000000000000000000, 1.000000000000000000 ) ) ;
#83198=PLANE ( 'NONE',  #34945 ) ;
#83200=ORIENTED_EDGE ( 'NONE', *, *, #7511, .F. ) ;
#83201=DIRECTION ( 'NONE',  ( -0.000000000000000000, -0.3543493200069152693, 0.9351131265310292928 ) ) ;
#83202=ORIENTED_EDGE ( 'NONE', *, *, #124220, .T. ) ;
#83203=ORIENTED_EDGE ( 'NONE', *, *, #112858, .F. ) ;
#83205=AXIS2_PLACEMENT_3D ( 'NONE', #42880, #99345, #132755 ) ;
#83206=ORIENTED_EDGE ( 'NONE', *, *, #89021, .T. ) ;
#83207=ORIENTED_EDGE ( 'NONE', *, *, #41600, .F. ) ;
#83209=VECTOR ( 'NONE', #77437, 1000.000000000000000 ) ;
#83210=ORIENTED_EDGE ( 'NONE', *, *, #79896, .F. ) ;
#83213=CARTESIAN_POINT ( 'NONE',  ( -78.18398860626899705, 28.73617430169841924, 5.000000000000000000 ) ) ;
#83215=DIRECTION ( 'NONE',  ( -0.6830127018922181881, 0.6830127018922202975, -0.2588190451025214056 ) ) ;
#83217=DIRECTION ( 'NONE',  ( 0.3543493200069163240, 0.000000000000000000, 0.9351131265310288487 ) ) ;
#83219=VECTOR ( 'NONE', #119075, 1000.000000000000000 ) ;
#83220=CARTESIAN_POINT ( 'NONE',  ( 25.49999999999982236, 7.466399257802184053, 5.000000000000000000 ) ) ;
#83221=CARTESIAN_POINT ( 'NONE',  ( -8.999999999999934275, 10.55218569542906337, 5.000000000000000000 ) ) ;
#83223=CARTESIAN_POINT ( 'NONE',  ( 34.42499999999998295, 4.541399257802000378, 5.000000000000000000 ) ) ;
#83226=DIRECTION ( 'NONE',  ( -0.7071067811865486830, -0.7071067811865464625, -0.000000000000000000 ) ) ;
#83227=VERTEX_POINT ( 'NONE', #54776 ) ;
#83231=LINE ( 'NONE', #40460, #63133 ) ;
#83233=EDGE_CURVE ( 'NONE', #10331, #102158, #86691, .T. ) ;
#83235=CARTESIAN_POINT ( 'NONE',  ( -36.69326993309576324, -3.740707523384241728, 12.88036043432876454 ) ) ;
#83238=VERTEX_POINT ( 'NONE', #56235 ) ;
#83239=EDGE_CURVE ( 'NONE', #128485, #9178, #43184, .T. ) ;
#83240=EDGE_CURVE ( 'NONE', #23165, #87414, #111255, .T. ) ;
#83242=CARTESIAN_POINT ( 'NONE',  ( 24.70710678118637560, -12.74070752338415602, 5.000000000000000000 ) ) ;
#83243=PLANE ( 'NONE',  #89878 ) ;
#83245=DIRECTION ( 'NONE',  ( -0.7071067811865486830, -0.7071067811865464625, 0.000000000000000000 ) ) ;
#83246=VERTEX_POINT ( 'NONE', #33048 ) ;
#83247=ORIENTED_EDGE ( 'NONE', *, *, #94851, .F. ) ;
#83248=ORIENTED_EDGE ( 'NONE', *, *, #75480, .F. ) ;
#83249=CARTESIAN_POINT ( 'NONE',  ( 13.49999999999991829, 13.08746187583911080, 4.000000000000000000 ) ) ;
#83250=CARTESIAN_POINT ( 'NONE',  ( 21.24169458425174284, 0.7592924766157173044, 14.37146558664978002 ) ) ;
#83251=PLANE ( 'NONE',  #14977 ) ;
#83252=LINE ( 'NONE', #113736, #40362 ) ;
#83253=DIRECTION ( 'NONE',  ( -0.000000000000000000, 0.000000000000000000, 1.000000000000000000 ) ) ;
#83254=LINE ( 'NONE', #39776, #117430 ) ;
#83255=EDGE_CURVE ( 'NONE', #53085, #4806, #77262, .T. ) ;
#83257=DIRECTION ( 'NONE',  ( 0.7071067811865487940, -0.7071067811865463515, 0.000000000000000000 ) ) ;
#83258=CARTESIAN_POINT ( 'NONE',  ( 3.469446951953614189E-15, -4.447814304570782973, 5.000000000000000000 ) ) ;
#83262=EDGE_CURVE ( 'NONE', #28630, #99304, #55489, .T. ) ;
#83263=VECTOR ( 'NONE', #83342, 1000.000000000000000 ) ;
#83264=CARTESIAN_POINT ( 'NONE',  ( 3.489213562373097322, -27.52281430457057709, 5.000000000000000000 ) ) ;
#83265=ORIENTED_EDGE ( 'NONE', *, *, #141672, .T. ) ;
#83267=FACE_OUTER_BOUND ( 'NONE', #59976, .T. ) ;
#83269=EDGE_LOOP ( 'NONE', ( #36700, #117932, #23634 ) ) ;
#83271=CARTESIAN_POINT ( 'NONE',  ( -8.671830600776406328, -6.740707523384212863, 4.000000000000000000 ) ) ;
#83272=ADVANCED_FACE ( 'NONE', ( #349 ), #44645, .F. ) ;
#83273=VERTEX_POINT ( 'NONE', #45346 ) ;
#83274=ADVANCED_FACE ( 'NONE', ( #1059 ), #26418, .F. ) ;
#83275=AXIS2_PLACEMENT_3D ( 'NONE', #45516, #78127, #90410 ) ;
#83276=VERTEX_POINT ( 'NONE', #57639 ) ;
#83279=CARTESIAN_POINT ( 'NONE',  ( 42.18398860626899705, 28.73617430169816700, 5.000000000000000000 ) ) ;
#83280=AXIS2_PLACEMENT_3D ( 'NONE', #108886, #109628, #118353 ) ;
#83281=LINE ( 'NONE', #16568, #76049 ) ;
#83282=CARTESIAN_POINT ( 'NONE',  ( -28.49999999999980460, -7.533600742197660516, 5.000000000000000000 ) ) ;
#83283=DIRECTION ( 'NONE',  ( -0.000000000000000000, -0.3543493200069152693, 0.9351131265310292928 ) ) ;
#83284=EDGE_CURVE ( 'NONE', #3074, #113572, #13364, .T. ) ;
#83285=DIRECTION ( 'NONE',  ( -0.7071067811865486830, -0.7071067811865464625, 0.000000000000000000 ) ) ;
#83289=CARTESIAN_POINT ( 'NONE',  ( 72.18398860626899705, 28.73617430169837661, 5.000000000000000000 ) ) ;
#83291=DIRECTION ( 'NONE',  ( -0.3543493200069162685, -0.000000000000000000, -0.9351131265310288487 ) ) ;
#83292=PLANE ( 'NONE',  #13107 ) ;
#83293=ORIENTED_EDGE ( 'NONE', *, *, #125676, .F. ) ;
#83294=EDGE_CURVE ( 'NONE', #122295, #1343, #138955, .T. ) ;
#83295=ORIENTED_EDGE ( 'NONE', *, *, #46206, .T. ) ;
#83296=EDGE_CURVE ( 'NONE', #398, #108741, #80111, .T. ) ;
#83298=VECTOR ( 'NONE', #134687, 1000.000000000000000 ) ;
#83299=DIRECTION ( 'NONE',  ( -0.000000000000000000, 0.000000000000000000, 1.000000000000000000 ) ) ;
#83300=ORIENTED_EDGE ( 'NONE', *, *, #51867, .T. ) ;
#83301=CARTESIAN_POINT ( 'NONE',  ( 11.27718569542934191, -21.72500000000000853, 5.000000000000000000 ) ) ;
#83302=CARTESIAN_POINT ( 'NONE',  ( 44.99451991528749772, 28.92564299267969474, 4.000000000000000000 ) ) ;
#83304=ORIENTED_EDGE ( 'NONE', *, *, #85527, .T. ) ;
#83305=AXIS2_PLACEMENT_3D ( 'NONE', #92226, #125612, #83536 ) ;
#83306=PLANE ( 'NONE',  #85653 ) ;
#83307=AXIS2_PLACEMENT_3D ( 'NONE', #83487, #127703, #50845 ) ;
#83308=EDGE_CURVE ( 'NONE', #133790, #25758, #12662, .T. ) ;
#83309=CARTESIAN_POINT ( 'NONE',  ( -34.47516574401891631, 3.028067341115791233, 4.998110765256836174 ) ) ;
#83312=DIRECTION ( 'NONE',  ( 0.7071067811865486830, -0.7071067811865464625, -0.000000000000000000 ) ) ;
#83313=ADVANCED_FACE ( 'NONE', ( #3889 ), #125740, .F. ) ;
#83314=AXIS2_PLACEMENT_3D ( 'NONE', #20830, #31030, #52744 ) ;
#83316=CARTESIAN_POINT ( 'NONE',  ( 72.29974487139158157, -27.71228299555256669, 4.000000000000000000 ) ) ;
#83317=VECTOR ( 'NONE', #16218, 1000.000000000000000 ) ;
#83318=CARTESIAN_POINT ( 'NONE',  ( -33.29974487139158867, -27.71228299555229313, 4.000000000000000000 ) ) ;
#83319=LINE ( 'NONE', #62286, #26212 ) ;
#83321=LINE ( 'NONE', #15860, #42952 ) ;
#83322=LINE ( 'NONE', #128258, #139518 ) ;
#83323=ORIENTED_EDGE ( 'NONE', *, *, #84374, .F. ) ;
#83324=EDGE_LOOP ( 'NONE', ( #133845, #72250, #122643, #120103 ) ) ;
#83326=ORIENTED_EDGE ( 'NONE', *, *, #36894, .T. ) ;
#83327=EDGE_CURVE ( 'NONE', #75885, #123393, #1752, .T. ) ;
#83329=AXIS2_PLACEMENT_3D ( 'NONE', #23909, #68171, #134836 ) ;
#83330=CARTESIAN_POINT ( 'NONE',  ( -54.48921356237310221, -27.52281430457093236, 5.000000000000000000 ) ) ;
#83331=ORIENTED_EDGE ( 'NONE', *, *, #104100, .T. ) ;
#83333=CARTESIAN_POINT ( 'NONE',  ( -63.18398860626900415, 28.73617430169831621, 5.000000000000000000 ) ) ;
#83334=CARTESIAN_POINT ( 'NONE',  ( 13.08316395874281568, 3.014287036135060660, 4.000000000000000000 ) ) ;
#83336=ORIENTED_EDGE ( 'NONE', *, *, #73139, .F. ) ;
#83337=CARTESIAN_POINT ( 'NONE',  ( -8.994519915287490619, 28.92564299267944250, 4.000000000000000000 ) ) ;
#83338=VERTEX_POINT ( 'NONE', #135886 ) ;
#83339=CARTESIAN_POINT ( 'NONE',  ( 1.828169399223523284, 6.759292476615653023, 4.000000000000000000 ) ) ;
#83340=AXIS2_PLACEMENT_3D ( 'NONE', #12596, #90909, #101031 ) ;
#83341=LINE ( 'NONE', #72505, #10718 ) ;
#83342=DIRECTION ( 'NONE',  ( 0.7071067811865486830, -0.7071067811865464625, -0.000000000000000000 ) ) ;
#83343=ORIENTED_EDGE ( 'NONE', *, *, #89372, .F. ) ;
#83344=EDGE_LOOP ( 'NONE', ( #20623, #66671, #80416, #12617 ) ) ;
#83345=ORIENTED_EDGE ( 'NONE', *, *, #41306, .T. ) ;
#83346=CARTESIAN_POINT ( 'NONE',  ( -31.49999999999977973, 21.43112307739196964, 4.000000000000000000 ) ) ;
#83347=FACE_OUTER_BOUND ( 'NONE', #113878, .T. ) ;
#83349=FACE_OUTER_BOUND ( 'NONE', #122854, .T. ) ;
#83350=EDGE_CURVE ( 'NONE', #111254, #64560, #14814, .T. ) ;
#83351=EDGE_CURVE ( 'NONE', #137064, #29922, #35175, .T. ) ;
#83352=DIRECTION ( 'NONE',  ( -0.7071067811865487940, 0.7071067811865463515, -0.000000000000000000 ) ) ;
#83353=VERTEX_POINT ( 'NONE', #135206 ) ;
#83356=EDGE_LOOP ( 'NONE', ( #11545, #47593, #58913, #44810, #137301 ) ) ;
#83357=ORIENTED_EDGE ( 'NONE', *, *, #30291, .F. ) ;
#83360=VECTOR ( 'NONE', #72945, 1000.000000000000000 ) ;
#83361=LINE ( 'NONE', #114541, #74398 ) ;
#83362=FACE_OUTER_BOUND ( 'NONE', #97969, .T. ) ;
#83363=EDGE_LOOP ( 'NONE', ( #50278, #99956, #91950, #124329 ) ) ;
#83364=CARTESIAN_POINT ( 'NONE',  ( -13.49999999999990763, -1.592773361805379428, -6.492772025301195349 ) ) ;
#83365=DIRECTION ( 'NONE',  ( -0.3543493200069162685, -0.000000000000000000, -0.9351131265310288487 ) ) ;
#83366=CARTESIAN_POINT ( 'NONE',  ( 0.000000000000000000, 0.000000000000000000, 5.000000000000000000 ) ) ;
#83368=VECTOR ( 'NONE', #60102, 1000.000000000000000 ) ;
#83371=VERTEX_POINT ( 'NONE', #4584 ) ;
#83372=AXIS2_PLACEMENT_3D ( 'NONE', #53053, #42221, #130660 ) ;
#83373=DIRECTION ( 'NONE',  ( 0.7071067811865487940, 0.7071067811865463515, 0.000000000000000000 ) ) ;
#83374=FACE_BOUND ( 'NONE', #53218, .T. ) ;
#83375=EDGE_LOOP ( 'NONE', ( #6841, #11004, #143225, #23866, #81403, #69884 ) ) ;
#83376=DIRECTION ( 'NONE',  ( -0.6830127018922180770, -0.6830127018922204085, -0.2588190451025213501 ) ) ;
#83377=CARTESIAN_POINT ( 'NONE',  ( 25.49999999999983302, 22.08746187583901843, 4.000000000000000000 ) ) ;
#83379=ORIENTED_EDGE ( 'NONE', *, *, #125346, .F. ) ;
#83380=DIRECTION ( 'NONE',  ( 0.3543493200069163240, 0.000000000000000000, -0.9351131265310288487 ) ) ;
#83381=ORIENTED_EDGE ( 'NONE', *, *, #102895, .T. ) ;
#83382=ORIENTED_EDGE ( 'NONE', *, *, #19049, .F. ) ;
#83383=VECTOR ( 'NONE', #87405, 1000.000000000000227 ) ;
#83384=ORIENTED_EDGE ( 'NONE', *, *, #94830, .T. ) ;
#83386=EDGE_LOOP ( 'NONE', ( #49269, #45461, #118131, #61842 ) ) ;
#83387=LINE ( 'NONE', #38453, #113196 ) ;
#83388=CARTESIAN_POINT ( 'NONE',  ( -3.489213562373097322, -27.52281430457057709, 5.000000000000000000 ) ) ;
#83389=DIRECTION ( 'NONE',  ( -0.7071067811865486830, -0.7071067811865464625, -0.000000000000000000 ) ) ;
#83391=EDGE_CURVE ( 'NONE', #47602, #118704, #101103, .T. ) ;
#83392=DIRECTION ( 'NONE',  ( 0.7071067811865487940, -0.7071067811865463515, 0.000000000000000000 ) ) ;
#83393=VECTOR ( 'NONE', #96942, 1000.000000000000000 ) ;
#83394=LINE ( 'NONE', #63092, #100151 ) ;
#83397=CARTESIAN_POINT ( 'NONE',  ( 9.473360963642086574, -5.240707523384232402, 16.25846745537497995 ) ) ;
#83398=FACE_OUTER_BOUND ( 'NONE', #108347, .T. ) ;
#83399=VERTEX_POINT ( 'NONE', #35893 ) ;
#83400=VECTOR ( 'NONE', #9817, 1000.000000000000000 ) ;
#83401=ORIENTED_EDGE ( 'NONE', *, *, #60897, .T. ) ;
#83403=ORIENTED_EDGE ( 'NONE', *, *, #120092, .T. ) ;
#83404=DIRECTION ( 'NONE',  ( 0.7071067811865487940, 0.7071067811865463515, 0.000000000000000000 ) ) ;
#83405=ORIENTED_EDGE ( 'NONE', *, *, #20383, .T. ) ;
#83407=ADVANCED_FACE ( 'NONE', ( #37290 ), #81539, .F. ) ;
#83408=VERTEX_POINT ( 'NONE', #24271 ) ;
#83409=DIRECTION ( 'NONE',  ( 0.000000000000000000, 0.000000000000000000, -1.000000000000000000 ) ) ;
#83410=DIRECTION ( 'NONE',  ( -0.6830127018922180770, -0.6830127018922204085, -0.2588190451025213501 ) ) ;
#83411=EDGE_CURVE ( 'NONE', #25811, #118828, #134473, .T. ) ;
#83412=ADVANCED_FACE ( 'NONE', ( #93096 ), #47501, .F. ) ;
#83413=VECTOR ( 'NONE', #126558, 1000.000000000000000 ) ;
#83414=FACE_OUTER_BOUND ( 'NONE', #5075, .T. ) ;
#83415=VERTEX_POINT ( 'NONE', #91662 ) ;
#83416=DIRECTION ( 'NONE',  ( 0.3543493200069164351, 2.781805975412904658E-17, -0.9351131265310288487 ) ) ;
#83417=ORIENTED_EDGE ( 'NONE', *, *, #133286, .F. ) ;
#83418=FACE_OUTER_BOUND ( 'NONE', #99472, .T. ) ;
#83420=EDGE_CURVE ( 'NONE', #91475, #98898, #125005, .T. ) ;
#83421=CARTESIAN_POINT ( 'NONE',  ( 34.92499999999998295, 8.816654386410357702, 4.500000000000000888 ) ) ;
#83422=AXIS2_PLACEMENT_3D ( 'NONE', #6817, #95295, #96002 ) ;
#83424=VERTEX_POINT ( 'NONE', #128577 ) ;
#83426=DIRECTION ( 'NONE',  ( -0.6830127018922181881, 0.6830127018922202975, -0.2588190451025214056 ) ) ;
#83427=EDGE_CURVE ( 'NONE', #100333, #11776, #115510, .T. ) ;
#83429=VERTEX_POINT ( 'NONE', #138752 ) ;
#83431=LINE ( 'NONE', #126894, #40371 ) ;
#83432=VECTOR ( 'NONE', #119801, 1000.000000000000000 ) ;
#83435=CARTESIAN_POINT ( 'NONE',  ( -11.99999999999991296, 1.761378380278670663, -6.096875308897281798 ) ) ;
#83436=CARTESIAN_POINT ( 'NONE',  ( 14.20710678118644665, -8.240707523384200428, 5.000000000000000000 ) ) ;
#83438=VERTEX_POINT ( 'NONE', #40857 ) ;
#83439=DIRECTION ( 'NONE',  ( 0.7071067811865486830, -0.7071067811865464625, -0.000000000000000000 ) ) ;
#83440=EDGE_CURVE ( 'NONE', #93458, #85512, #40177, .T. ) ;
#83441=CARTESIAN_POINT ( 'NONE',  ( 0.000000000000000000, 0.000000000000000000, 5.000000000000000000 ) ) ;
#83442=VERTEX_POINT ( 'NONE', #72097 ) ;
#83443=CARTESIAN_POINT ( 'NONE',  ( 6.792893218813413014, -8.240707523384202204, 5.000000000000000000 ) ) ;
#83445=CARTESIAN_POINT ( 'NONE',  ( -33.48921356237309510, -27.52281430457078670, 5.000000000000000000 ) ) ;
#83447=FACE_OUTER_BOUND ( 'NONE', #986, .T. ) ;
#83448=VERTEX_POINT ( 'NONE', #85063 ) ;
#83449=ORIENTED_EDGE ( 'NONE', *, *, #109740, .T. ) ;
#83450=LINE ( 'NONE', #59572, #97992 ) ;
#83451=ADVANCED_FACE ( 'NONE', ( #73494 ), #83676, .F. ) ;
#83452=VECTOR ( 'NONE', #80107, 1000.000000000000000 ) ;
#83453=ORIENTED_EDGE ( 'NONE', *, *, #71048, .F. ) ;
#83454=DIRECTION ( 'NONE',  ( 0.7071067811865486830, -0.7071067811865464625, -0.000000000000000000 ) ) ;
#83455=CARTESIAN_POINT ( 'NONE',  ( 27.18398860626900060, 28.73617430169806042, 5.000000000000000000 ) ) ;
#83457=ORIENTED_EDGE ( 'NONE', *, *, #25896, .T. ) ;
#83458=FACE_OUTER_BOUND ( 'NONE', #134488, .T. ) ;
#83459=LINE ( 'NONE', #28367, #113545 ) ;
#83462=EDGE_CURVE ( 'NONE', #66788, #108741, #127134, .T. ) ;
#83463=CARTESIAN_POINT ( 'NONE',  ( 11.29298673570687050, -21.74070752338406365, 4.999753212805220670 ) ) ;
#83464=FACE_OUTER_BOUND ( 'NONE', #62014, .T. ) ;
#83465=VECTOR ( 'NONE', #58661, 1000.000000000000000 ) ;
#83468=EDGE_LOOP ( 'NONE', ( #124094, #31917, #101491, #69173 ) ) ;
#83469=( BOUNDED_CURVE ( )  B_SPLINE_CURVE ( 3, ( #61000, #138514, #94975, #27587 ),
 .UNSPECIFIED., .F., .F. ) 
 B_SPLINE_CURVE_WITH_KNOTS ( ( 4, 4 ),
 ( 1.964434688349496083, 3.503810798801452187 ),
 .UNSPECIFIED. ) 
 CURVE ( )  GEOMETRIC_REPRESENTATION_ITEM ( )  RATIONAL_B_SPLINE_CURVE ( ( 1.000000000000000000, 0.8120851936182298392, 0.8120851936182298392, 1.000000000000000000 ) ) 
 REPRESENTATION_ITEM ( '' )  );
#83470=ORIENTED_EDGE ( 'NONE', *, *, #108740, .T. ) ;
#83471=ORIENTED_EDGE ( 'NONE', *, *, #36274, .F. ) ;
#83472=ADVANCED_FACE ( 'NONE', ( #49628 ), #84387, .F. ) ;
#83474=AXIS2_PLACEMENT_3D ( 'NONE', #21292, #85111, #129319 ) ;
#83475=ORIENTED_EDGE ( 'NONE', *, *, #67997, .F. ) ;
#83476=VERTEX_POINT ( 'NONE', #5342 ) ;
#83478=VERTEX_POINT ( 'NONE', #93802 ) ;
#83479=DIRECTION ( 'NONE',  ( 0.7071067811865487940, 0.7071067811865463515, -0.000000000000000000 ) ) ;
#83480=LINE ( 'NONE', #137867, #30073 ) ;
#83481=VECTOR ( 'NONE', #72402, 1000.000000000000000 ) ;
#83483=VECTOR ( 'NONE', #93409, 1000.000000000000000 ) ;
#83484=VECTOR ( 'NONE', #113631, 1000.000000000000000 ) ;
#83485=ORIENTED_EDGE ( 'NONE', *, *, #61257, .T. ) ;
#83486=( BOUNDED_CURVE ( )  B_SPLINE_CURVE ( 3, ( #57843, #68709, #102033, #90439 ),
 .UNSPECIFIED., .F., .T. ) 
 B_SPLINE_CURVE_WITH_KNOTS ( ( 4, 4 ),
 ( 0.4286956587950770392, 0.5111536932531050015 ),
 .UNSPECIFIED. ) 
 CURVE ( )  GEOMETRIC_REPRESENTATION_ITEM ( )  RATIONAL_B_SPLINE_CURVE ( ( 1.000000000000000000, 0.9994334696367943582, 0.9994334696367943582, 1.000000000000000000 ) ) 
 REPRESENTATION_ITEM ( '' )  );
#83487=CARTESIAN_POINT ( 'NONE',  ( 0.000000000000000000, 0.000000000000000000, 5.000000000000000000 ) ) ;
#83488=EDGE_CURVE ( 'NONE', #72014, #105080, #29958, .T. ) ;
#83489=VECTOR ( 'NONE', #66114, 999.9999999999998863 ) ;
#83491=DIRECTION ( 'NONE',  ( -0.000000000000000000, -0.3543493200069152693, 0.9351131265310292928 ) ) ;
#83492=PLANE ( 'NONE',  #90483 ) ;
#83494=VERTEX_POINT ( 'NONE', #106070 ) ;
#83496=DIRECTION ( 'NONE',  ( 0.7071067811865487940, 0.7071067811865463515, -0.000000000000000000 ) ) ;
#83498=CARTESIAN_POINT ( 'NONE',  ( -2.999999999999981792, 5.966399257802200040, 5.000000000000000000 ) ) ;
#83500=EDGE_CURVE ( 'NONE', #77065, #77128, #39449, .T. ) ;
#83501=PLANE ( 'NONE',  #123304 ) ;
#83502=CARTESIAN_POINT ( 'NONE',  ( -5.163471288734476694, 15.75929247661555976, 9.299976744542908236 ) ) ;
#83504=FACE_OUTER_BOUND ( 'NONE', #128002, .T. ) ;
#83506=EDGE_LOOP ( 'NONE', ( #26579, #17552, #9333, #90975 ) ) ;
#83507=ORIENTED_EDGE ( 'NONE', *, *, #135008, .T. ) ;
#83509=ORIENTED_EDGE ( 'NONE', *, *, #574, .F. ) ;
#83510=EDGE_CURVE ( 'NONE', #1974, #55061, #28565, .T. ) ;
#83512=VECTOR ( 'NONE', #120690, 1000.000000000000000 ) ;
#83514=CARTESIAN_POINT ( 'NONE',  ( 25.99384647351989130, 22.22500000000000142, -18.08442819488239195 ) ) ;
#83515=CARTESIAN_POINT ( 'NONE',  ( -9.183988606268997046, 28.73617430169793607, 5.000000000000000000 ) ) ;
#83516=CARTESIAN_POINT ( 'NONE',  ( -22.82816939922337340, -20.24070752338407075, 4.000000000000000000 ) ) ;
#83517=DIRECTION ( 'NONE',  ( 0.7071067811865487940, 0.7071067811865463515, 0.000000000000000000 ) ) ;
#83519=VECTOR ( 'NONE', #75538, 1000.000000000000000 ) ;
#83521=EDGE_CURVE ( 'NONE', #28383, #21537, #62621, .T. ) ;
#83523=VECTOR ( 'NONE', #60324, 1000.000000000000227 ) ;
#83524=CARTESIAN_POINT ( 'NONE',  ( -25.49999999999981881, 4.466399257802215139, 5.000000000000000000 ) ) ;
#83525=ORIENTED_EDGE ( 'NONE', *, *, #47910, .T. ) ;
#83526=CARTESIAN_POINT ( 'NONE',  ( -33.29974487139158867, -27.71228299555229313, 4.000000000000000000 ) ) ;
#83527=VECTOR ( 'NONE', #122120, 1000.000000000000000 ) ;
#83528=CARTESIAN_POINT ( 'NONE',  ( -28.17183060077627133, -14.24070752338413648, 4.000000000000000000 ) ) ;
#83529=CARTESIAN_POINT ( 'NONE',  ( -4.499999999999966249, -2.947814304570802513, 5.000000000000000000 ) ) ;
#83531=VERTEX_POINT ( 'NONE', #61236 ) ;
#83532=EDGE_CURVE ( 'NONE', #89577, #9427, #29251, .T. ) ;
#83534=VERTEX_POINT ( 'NONE', #105381 ) ;
#83535=DIRECTION ( 'NONE',  ( 0.7071067811865487940, 0.7071067811865463515, 0.000000000000000000 ) ) ;
#83536=DIRECTION ( 'NONE',  ( 1.000000000000000000, 0.000000000000000000, 0.000000000000000000 ) ) ;
#83537=ADVANCED_FACE ( 'NONE', ( #19095 ), #50313, .F. ) ;
#83538=CARTESIAN_POINT ( 'NONE',  ( 36.48921356237310221, -27.52281430457080802, 5.000000000000000000 ) ) ;
#83539=CARTESIAN_POINT ( 'NONE',  ( 32.21837311707483309, 21.74787736706806740, 4.999607392498048419 ) ) ;
#83540=EDGE_CURVE ( 'NONE', #44583, #136777, #61916, .T. ) ;
#83541=AXIS2_PLACEMENT_3D ( 'NONE', #86500, #118379, #39433 ) ;
#83544=ORIENTED_EDGE ( 'NONE', *, *, #112372, .F. ) ;
#83545=DIRECTION ( 'NONE',  ( 0.7071067811865486830, -0.7071067811865464625, -0.000000000000000000 ) ) ;
#83546=LINE ( 'NONE', #127754, #8514 ) ;
#83547=ORIENTED_EDGE ( 'NONE', *, *, #4330, .T. ) ;
#83548=ORIENTED_EDGE ( 'NONE', *, *, #134654, .F. ) ;
#83549=VECTOR ( 'NONE', #56607, 1000.000000000000227 ) ;
#83550=CARTESIAN_POINT ( 'NONE',  ( -21.32816939922338406, 11.25929247661560240, 4.000000000000000000 ) ) ;
#83551=ORIENTED_EDGE ( 'NONE', *, *, #94880, .T. ) ;
#83552=EDGE_CURVE ( 'NONE', #89048, #108692, #22627, .T. ) ;
#83553=LINE ( 'NONE', #61126, #30624 ) ;
#83555=EDGE_LOOP ( 'NONE', ( #114808, #134262, #108253, #44325 ) ) ;
#83556=AXIS2_PLACEMENT_3D ( 'NONE', #38310, #25271, #69530 ) ;
#83557=DIRECTION ( 'NONE',  ( 0.7071067811865486830, -0.7071067811865464625, -0.000000000000000000 ) ) ;
#83558=FACE_BOUND ( 'NONE', #96339, .T. ) ;
#83559=EDGE_CURVE ( 'NONE', #115805, #122150, #65497, .T. ) ;
#83560=CARTESIAN_POINT ( 'NONE',  ( -17.99999999999986855, 10.55218569542905804, 5.000000000000000000 ) ) ;
#83561=FACE_OUTER_BOUND ( 'NONE', #988, .T. ) ;
#83562=DIRECTION ( 'NONE',  ( 0.7071067811865486830, -0.7071067811865464625, -0.000000000000000000 ) ) ;
#83563=EDGE_LOOP ( 'NONE', ( #132433, #59590, #96502, #66791, #1134 ) ) ;
#83565=DIRECTION ( 'NONE',  ( 0.7071067811865486830, -0.7071067811865464625, -0.000000000000000000 ) ) ;
#83567=ORIENTED_EDGE ( 'NONE', *, *, #101946, .T. ) ;
#83568=VECTOR ( 'NONE', #11761, 1000.000000000000000 ) ;
#83570=ORIENTED_EDGE ( 'NONE', *, *, #19857, .F. ) ;
#83571=VERTEX_POINT ( 'NONE', #53134 ) ;
#83573=ORIENTED_EDGE ( 'NONE', *, *, #53699, .T. ) ;
#83575=FACE_OUTER_BOUND ( 'NONE', #69499, .T. ) ;
#83576=ORIENTED_EDGE ( 'NONE', *, *, #58108, .T. ) ;
#83577=VECTOR ( 'NONE', #2983, 1000.000000000000000 ) ;
#83578=VECTOR ( 'NONE', #92446, 1000.000000000000000 ) ;
#83579=VECTOR ( 'NONE', #126309, 1000.000000000000000 ) ;
#83583=LINE ( 'NONE', #37201, #49331 ) ;
#83584=EDGE_CURVE ( 'NONE', #80245, #13520, #87922, .T. ) ;
#83585=ORIENTED_EDGE ( 'NONE', *, *, #125783, .T. ) ;
#83586=AXIS2_PLACEMENT_3D ( 'NONE', #28522, #81490, #16917 ) ;
#83587=VECTOR ( 'NONE', #28558, 999.9999999999998863 ) ;
#83590=VECTOR ( 'NONE', #79651, 1000.000000000000000 ) ;
#83591=CARTESIAN_POINT ( 'NONE',  ( -4.499999999999966249, -1.912538124160739095, 4.000000000000000000 ) ) ;
#83592=FACE_OUTER_BOUND ( 'NONE', #96051, .T. ) ;
#83593=EDGE_LOOP ( 'NONE', ( #86874, #142381, #133088, #127054 ) ) ;
#83595=ORIENTED_EDGE ( 'NONE', *, *, #81534, .T. ) ;
#83596=EDGE_LOOP ( 'NONE', ( #48389, #10960, #27957, #87258 ) ) ;
#83597=LINE ( 'NONE', #28497, #23464 ) ;
#83598=DIRECTION ( 'NONE',  ( 0.7071067811865486830, -0.7071067811865464625, -0.000000000000000000 ) ) ;
#83599=EDGE_CURVE ( 'NONE', #58716, #88957, #87215, .T. ) ;
#83600=DIRECTION ( 'NONE',  ( 0.7071067811865487940, 0.7071067811865463515, 0.000000000000000000 ) ) ;
#83601=EDGE_LOOP ( 'NONE', ( #138451, #83945, #69318, #80514 ) ) ;
#83602=VECTOR ( 'NONE', #42679, 1000.000000000000227 ) ;
#83603=FACE_OUTER_BOUND ( 'NONE', #66315, .T. ) ;
#83605=ADVANCED_FACE ( 'NONE', ( #111073 ), #110363, .F. ) ;
#83606=ADVANCED_FACE ( 'NONE', ( #77081 ), #42306, .F. ) ;
#83609=EDGE_CURVE ( 'NONE', #139694, #105592, #10211, .T. ) ;
#83610=VERTEX_POINT ( 'NONE', #158 ) ;
#83611=DIRECTION ( 'NONE',  ( 0.3543493200069162685, -0.000000000000000000, -0.9351131265310288487 ) ) ;
#83612=AXIS2_PLACEMENT_3D ( 'NONE', #97034, #107920, #99754 ) ;
#83613=EDGE_CURVE ( 'NONE', #94785, #120961, #31412, .T. ) ;
#83614=CARTESIAN_POINT ( 'NONE',  ( -28.22850677138647768, 20.25929247661551358, 7.808871592221704461 ) ) ;
#83615=VECTOR ( 'NONE', #95016, 1000.000000000000000 ) ;
#83616=CARTESIAN_POINT ( 'NONE',  ( 0.000000000000000000, 21.72500000000000142, 4.500000000000000888 ) ) ;
#83618=ORIENTED_EDGE ( 'NONE', *, *, #138625, .T. ) ;
#83619=CARTESIAN_POINT ( 'NONE',  ( 10.49999999999993250, 10.46639925780215563, 5.000000000000000000 ) ) ;
#83620=ORIENTED_EDGE ( 'NONE', *, *, #112271, .T. ) ;
#83622=LINE ( 'NONE', #127832, #135275 ) ;
#83623=DIRECTION ( 'NONE',  ( -0.6830127018922180770, -0.6830127018922204085, -0.2588190451025213501 ) ) ;
#83624=DIRECTION ( 'NONE',  ( 1.000000000000000000, 0.000000000000000000, 0.000000000000000000 ) ) ;
#83626=AXIS2_PLACEMENT_3D ( 'NONE', #74271, #118462, #19162 ) ;
#83627=EDGE_CURVE ( 'NONE', #142445, #88361, #86516, .T. ) ;
#83628=VECTOR ( 'NONE', #100969, 1000.000000000000000 ) ;
#83629=AXIS2_PLACEMENT_3D ( 'NONE', #132630, #77524, #67353 ) ;
#83630=DIRECTION ( 'NONE',  ( 0.7071067811865487940, 0.7071067811865463515, 0.000000000000000000 ) ) ;
#83632=DIRECTION ( 'NONE',  ( 0.6830127018922180770, -0.6830127018922204085, -0.2588190451025213501 ) ) ;
#83633=ORIENTED_EDGE ( 'NONE', *, *, #51685, .T. ) ;
#83634=LINE ( 'NONE', #106032, #92455 ) ;
#83636=LINE ( 'NONE', #28527, #7611 ) ;
#83637=CARTESIAN_POINT ( 'NONE',  ( 5.356812572482577472, -20.24070752338407786, 21.22881796311214231 ) ) ;
#83638=EDGE_CURVE ( 'NONE', #67930, #11479, #43707, .T. ) ;
#83639=CARTESIAN_POINT ( 'NONE',  ( -42.48921356237308800, -27.52281430457085065, 5.000000000000000000 ) ) ;
#83640=CARTESIAN_POINT ( 'NONE',  ( 11.99999999999992539, -0.03360074219773377668, 5.000000000000000000 ) ) ;
#83641=ORIENTED_EDGE ( 'NONE', *, *, #9914, .F. ) ;
#83643=EDGE_LOOP ( 'NONE', ( #44701, #104279, #89422, #90913 ) ) ;
#83644=CARTESIAN_POINT ( 'NONE',  ( -39.48921356237310221, -27.52281430457082934, 5.000000000000000000 ) ) ;
#83649=VECTOR ( 'NONE', #109658, 999.9999999999998863 ) ;
#83650=DIRECTION ( 'NONE',  ( -0.7071067811865486830, -0.7071067811865464625, -0.000000000000000000 ) ) ;
#83651=CARTESIAN_POINT ( 'NONE',  ( 34.42499999999998295, -13.45860074219782021, 5.000000000000000000 ) ) ;
#83652=DIRECTION ( 'NONE',  ( -0.6830127018922180770, -0.6830127018922204085, -0.2588190451025213501 ) ) ;
#83653=ORIENTED_EDGE ( 'NONE', *, *, #53172, .T. ) ;
#83654=CARTESIAN_POINT ( 'NONE',  ( 36.48921356237310221, -27.52281430457080802, 5.000000000000000000 ) ) ;
#83657=DIRECTION ( 'NONE',  ( -0.7071067811865487940, 0.7071067811865463515, 0.000000000000000000 ) ) ;
#83658=VECTOR ( 'NONE', #122279, 1000.000000000000000 ) ;
#83659=DIRECTION ( 'NONE',  ( 0.7071067811865487940, 0.7071067811865463515, 0.000000000000000000 ) ) ;
#83661=LINE ( 'NONE', #47486, #55684 ) ;
#83662=ORIENTED_EDGE ( 'NONE', *, *, #88385, .F. ) ;
#83664=ORIENTED_EDGE ( 'NONE', *, *, #70832, .T. ) ;
#83665=VECTOR ( 'NONE', #120173, 1000.000000000000000 ) ;
#83666=ADVANCED_FACE ( 'NONE', ( #121257 ), #97339, .T. ) ;
#83667=ORIENTED_EDGE ( 'NONE', *, *, #78185, .F. ) ;
#83668=VECTOR ( 'NONE', #97112, 1000.000000000000000 ) ;
#83669=CARTESIAN_POINT ( 'NONE',  ( -1.499999999999994449, 8.900465351122148761, -2.516491619111509426 ) ) ;
#83670=EDGE_CURVE ( 'NONE', #128517, #97084, #131439, .T. ) ;
#83671=CARTESIAN_POINT ( 'NONE',  ( 60.48921356237309510, -27.52281430457097500, 5.000000000000000000 ) ) ;
#83673=CARTESIAN_POINT ( 'NONE',  ( -6.183988606268994381, 28.73617430169791476, 5.000000000000000000 ) ) ;
#83674=LINE ( 'NONE', #5339, #48788 ) ;
#83675=VERTEX_POINT ( 'NONE', #76344 ) ;
#83676=PLANE ( 'NONE',  #88056 ) ;
#83677=PLANE ( 'NONE',  #88548 ) ;
#83679=VECTOR ( 'NONE', #11586, 1000.000000000000000 ) ;
#83680=CARTESIAN_POINT ( 'NONE',  ( -3.489213562373097322, -27.52281430457057709, 5.000000000000000000 ) ) ;
#83681=DIRECTION ( 'NONE',  ( -0.7071067811865486830, -0.7071067811865464625, 0.000000000000000000 ) ) ;
#83682=EDGE_CURVE ( 'NONE', #98608, #137664, #120512, .T. ) ;
#83683=DIRECTION ( 'NONE',  ( -0.000000000000000000, -0.3543493200069152693, 0.9351131265310292928 ) ) ;
#83685=PLANE ( 'NONE',  #92271 ) ;
#83686=VERTEX_POINT ( 'NONE', #11037 ) ;
#83687=ORIENTED_EDGE ( 'NONE', *, *, #88675, .T. ) ;
#83689=FACE_OUTER_BOUND ( 'NONE', #66264, .T. ) ;
#83690=EDGE_CURVE ( 'NONE', #129163, #106470, #55313, .T. ) ;
#83691=CARTESIAN_POINT ( 'NONE',  ( -81.29974487139159578, -27.71228299555262709, 4.000000000000000000 ) ) ;
#83692=DIRECTION ( 'NONE',  ( -0.7071067811865486830, -0.7071067811865464625, 0.000000000000000000 ) ) ;
#83693=ORIENTED_EDGE ( 'NONE', *, *, #126223, .F. ) ;
#83694=VECTOR ( 'NONE', #141932, 1000.000000000000000 ) ;
#83695=DIRECTION ( 'NONE',  ( -0.000000000000000000, 0.000000000000000000, 1.000000000000000000 ) ) ;
#83696=VECTOR ( 'NONE', #54698, 1000.000000000000000 ) ;
#83697=VECTOR ( 'NONE', #139555, 1000.000000000000000 ) ;
#83698=CARTESIAN_POINT ( 'NONE',  ( -59.99451991528749772, 28.92564299267980132, 4.000000000000000000 ) ) ;
#83701=ORIENTED_EDGE ( 'NONE', *, *, #47947, .F. ) ;
#83703=ORIENTED_EDGE ( 'NONE', *, *, #127688, .F. ) ;
#83704=AXIS2_PLACEMENT_3D ( 'NONE', #37491, #114314, #14991 ) ;
#83706=AXIS2_PLACEMENT_3D ( 'NONE', #46283, #57868, #123109 ) ;
#83708=AXIS2_PLACEMENT_3D ( 'NONE', #79894, #24041, #36350 ) ;
#83710=CARTESIAN_POINT ( 'NONE',  ( -34.42500000000001137, 11.97718569542929856, 5.000000000000000000 ) ) ;
#83711=PLANE ( 'NONE',  #2327 ) ;
#83713=LINE ( 'NONE', #85806, #129856 ) ;
#83714=DIRECTION ( 'NONE',  ( 0.7071067811865487940, 0.7071067811865463515, 0.000000000000000000 ) ) ;
#83715=EDGE_LOOP ( 'NONE', ( #29710, #96247, #33593, #29528 ) ) ;
#83716=DIRECTION ( 'NONE',  ( 0.3543493200069162685, -0.000000000000000000, -0.9351131265310288487 ) ) ;
#83717=DIRECTION ( 'NONE',  ( -0.000000000000000000, 0.000000000000000000, 1.000000000000000000 ) ) ;
#83718=DIRECTION ( 'NONE',  ( -0.3543493200069162685, -0.000000000000000000, -0.9351131265310288487 ) ) ;
#83719=VECTOR ( 'NONE', #32896, 1000.000000000000000 ) ;
#83720=LINE ( 'NONE', #30004, #6733 ) ;
#83721=ORIENTED_EDGE ( 'NONE', *, *, #132431, .F. ) ;
#83722=EDGE_LOOP ( 'NONE', ( #66919, #126188, #10466, #6710 ) ) ;
#83724=DIRECTION ( 'NONE',  ( 0.7071067811865486830, -0.7071067811865464625, -0.000000000000000000 ) ) ;
#83725=DIRECTION ( 'NONE',  ( -0.7071067811865487940, 0.7071067811865463515, 0.000000000000000000 ) ) ;
#83726=CARTESIAN_POINT ( 'NONE',  ( 34.92499999999998295, -21.72500000000000142, 5.000000000000000000 ) ) ;
#83727=LINE ( 'NONE', #16249, #36297 ) ;
#83728=VERTEX_POINT ( 'NONE', #78487 ) ;
#83729=ORIENTED_EDGE ( 'NONE', *, *, #102605, .T. ) ;
#83730=FACE_OUTER_BOUND ( 'NONE', #113195, .T. ) ;
#83732=ORIENTED_EDGE ( 'NONE', *, *, #66664, .T. ) ;
#83733=EDGE_CURVE ( 'NONE', #98565, #114933, #79952, .T. ) ;
#83734=VECTOR ( 'NONE', #19524, 1000.000000000000000 ) ;
#83735=ORIENTED_EDGE ( 'NONE', *, *, #136119, .F. ) ;
#83736=VECTOR ( 'NONE', #43399, 1000.000000000000000 ) ;
#83737=ADVANCED_FACE ( 'NONE', ( #114655 ), #1592, .F. ) ;
#83738=DIRECTION ( 'NONE',  ( 0.3543493200069162685, -0.000000000000000000, -0.9351131265310288487 ) ) ;
#83739=ORIENTED_EDGE ( 'NONE', *, *, #52063, .T. ) ;
#83740=AXIS2_PLACEMENT_3D ( 'NONE', #17578, #93022, #1848 ) ;
#83741=LINE ( 'NONE', #129334, #78121 ) ;
#83742=DIRECTION ( 'NONE',  ( -0.000000000000000000, 0.000000000000000000, 1.000000000000000000 ) ) ;
#83743=AXIS2_PLACEMENT_3D ( 'NONE', #3548, #15832, #60129 ) ;
#83744=FACE_BOUND ( 'NONE', #53521, .T. ) ;
#83746=EDGE_CURVE ( 'NONE', #61121, #137089, #3726, .T. ) ;
#83747=CARTESIAN_POINT ( 'NONE',  ( 3.707013264293012256, -21.74070752338405654, 4.999753212805217117 ) ) ;
#83748=LINE ( 'NONE', #61984, #52817 ) ;
#83749=ORIENTED_EDGE ( 'NONE', *, *, #28317, .T. ) ;
#83750=DIRECTION ( 'NONE',  ( -0.7071067811865487940, 0.7071067811865463515, 0.000000000000000000 ) ) ;
#83752=ORIENTED_EDGE ( 'NONE', *, *, #22610, .T. ) ;
#83753=ORIENTED_EDGE ( 'NONE', *, *, #27667, .F. ) ;
#83755=ORIENTED_EDGE ( 'NONE', *, *, #59592, .T. ) ;
#83756=DIRECTION ( 'NONE',  ( 0.6830127018922180770, -0.6830127018922204085, -0.2588190451025213501 ) ) ;
#83757=VECTOR ( 'NONE', #79811, 999.9999999999998863 ) ;
#83758=CARTESIAN_POINT ( 'NONE',  ( 34.92499999999998295, 17.56110451772265080, 6.767324343803300835 ) ) ;
#83760=CARTESIAN_POINT ( 'NONE',  ( 8.994519915287490619, 28.92564299267944250, 4.000000000000000000 ) ) ;
#83761=DIRECTION ( 'NONE',  ( -0.000000000000000000, -0.3543493200069153803, -0.9351131265310292928 ) ) ;
#83762=ORIENTED_EDGE ( 'NONE', *, *, #86994, .F. ) ;
#83763=CARTESIAN_POINT ( 'NONE',  ( 30.29974487139158867, -27.71228299555227537, 4.000000000000000000 ) ) ;
#83764=LINE ( 'NONE', #127974, #52399 ) ;
#83765=LINE ( 'NONE', #138116, #45812 ) ;
#83766=AXIS2_PLACEMENT_3D ( 'NONE', #25252, #113694, #14386 ) ;
#83767=PLANE ( 'NONE',  #119100 ) ;
#83768=CARTESIAN_POINT ( 'NONE',  ( 21.48921356237309155, -27.52281430457070499, 5.000000000000000000 ) ) ;
#83770=AXIS2_PLACEMENT_3D ( 'NONE', #96572, #107485, #40815 ) ;
#83771=CARTESIAN_POINT ( 'NONE',  ( -34.92500000000001137, -9.183345613589475320, 4.500000000000000888 ) ) ;
#83772=ORIENTED_EDGE ( 'NONE', *, *, #92454, .F. ) ;
#83773=FACE_OUTER_BOUND ( 'NONE', #40743, .T. ) ;
#83775=ORIENTED_EDGE ( 'NONE', *, *, #106858, .F. ) ;
#83776=VERTEX_POINT ( 'NONE', #122682 ) ;
#83779=EDGE_LOOP ( 'NONE', ( #72747, #72372, #61735, #131002 ) ) ;
#83780=EDGE_CURVE ( 'NONE', #10035, #27758, #111832, .T. ) ;
#83783=ADVANCED_FACE ( 'NONE', ( #135039 ), #37109, .F. ) ;
#83784=ORIENTED_EDGE ( 'NONE', *, *, #137941, .F. ) ;
#83785=EDGE_CURVE ( 'NONE', #115183, #115678, #112532, .T. ) ;
#83787=ADVANCED_FACE ( 'NONE', ( #81365 ), #134301, .F. ) ;
#83788=ORIENTED_EDGE ( 'NONE', *, *, #91600, .F. ) ;
#83789=DIRECTION ( 'NONE',  ( -0.3543493200069162685, -0.000000000000000000, -0.9351131265310288487 ) ) ;
#83790=PLANE ( 'NONE',  #130820 ) ;
#83792=DIRECTION ( 'NONE',  ( 0.7071067811865487940, -0.7071067811865463515, 0.000000000000000000 ) ) ;
#83794=EDGE_LOOP ( 'NONE', ( #103630, #29780, #42878, #128319 ) ) ;
#83795=EDGE_CURVE ( 'NONE', #33310, #23228, #56775, .T. ) ;
#83796=CARTESIAN_POINT ( 'NONE',  ( -36.48921356237310221, -27.52281430457080802, 5.000000000000000000 ) ) ;
#83799=VECTOR ( 'NONE', #115406, 1000.000000000000227 ) ;
#83800=VERTEX_POINT ( 'NONE', #59609 ) ;
#83804=ORIENTED_EDGE ( 'NONE', *, *, #126486, .T. ) ;
#83805=EDGE_CURVE ( 'NONE', #20628, #35756, #35000, .T. ) ;
#83806=EDGE_LOOP ( 'NONE', ( #97768, #38186, #91854, #117590 ) ) ;
#83807=CARTESIAN_POINT ( 'NONE',  ( -42.29974487139158157, -27.71228299555235708, 4.000000000000000000 ) ) ;
#83808=VECTOR ( 'NONE', #124310, 1000.000000000000227 ) ;
#83809=VECTOR ( 'NONE', #29471, 1000.000000000000000 ) ;
#83810=LINE ( 'NONE', #128018, #56219 ) ;
#83811=EDGE_CURVE ( 'NONE', #65370, #24066, #45876, .T. ) ;
#83812=CARTESIAN_POINT ( 'NONE',  ( 25.49999999999982236, 4.087461875839204062, 4.000000000000000000 ) ) ;
#83813=LINE ( 'NONE', #104066, #20829 ) ;
#83814=ADVANCED_FACE ( 'NONE', ( #124835 ), #90803, .F. ) ;
#83816=CARTESIAN_POINT ( 'NONE',  ( 0.3281693992235289459, 14.25929247661556687, 4.000000000000000000 ) ) ;
#83817=VERTEX_POINT ( 'NONE', #57466 ) ;
#83818=CARTESIAN_POINT ( 'NONE',  ( -20.99999999999985079, -19.22509904557638549, 1.855685503482130239 ) ) ;
#83819=EDGE_CURVE ( 'NONE', #52354, #105598, #25894, .T. ) ;
#83821=CARTESIAN_POINT ( 'NONE',  ( 11.20710678118647330, -5.240707523384234179, 5.000000000000000000 ) ) ;
#83822=LINE ( 'NONE', #114938, #94625 ) ;
#83823=CARTESIAN_POINT ( 'NONE',  ( 0.000000000000000000, 0.000000000000000000, 5.000000000000000000 ) ) ;
#83824=ORIENTED_EDGE ( 'NONE', *, *, #90182, .T. ) ;
#83825=ORIENTED_EDGE ( 'NONE', *, *, #77518, .T. ) ;
#83826=ORIENTED_EDGE ( 'NONE', *, *, #136469, .F. ) ;
#83827=DIRECTION ( 'NONE',  ( -0.000000000000000000, -0.3543493200069152693, 0.9351131265310292928 ) ) ;
#83828=FACE_OUTER_BOUND ( 'NONE', #78075, .T. ) ;
#83830=DIRECTION ( 'NONE',  ( 0.7071067811865487940, 0.7071067811865463515, 0.000000000000000000 ) ) ;
#83831=CARTESIAN_POINT ( 'NONE',  ( -3.328169399223503966, -6.740707523384211086, 4.000000000000000000 ) ) ;
#83834=VECTOR ( 'NONE', #93353, 999.9999999999998863 ) ;
#83837=DIRECTION ( 'NONE',  ( 0.7071067811865487940, 0.7071067811865463515, 0.000000000000000000 ) ) ;
#83838=PLANE ( 'NONE',  #8419 ) ;
#83840=AXIS2_PLACEMENT_3D ( 'NONE', #114422, #136893, #16519 ) ;
#83841=FACE_OUTER_BOUND ( 'NONE', #66148, .T. ) ;
#83842=EDGE_CURVE ( 'NONE', #17057, #20345, #24802, .T. ) ;
#83843=ORIENTED_EDGE ( 'NONE', *, *, #116569, .T. ) ;
#83844=DIRECTION ( 'NONE',  ( -0.7071067811865486830, -0.7071067811865464625, 0.000000000000000000 ) ) ;
#83845=VECTOR ( 'NONE', #49085, 1000.000000000000000 ) ;
#83846=EDGE_LOOP ( 'NONE', ( #133704, #97601, #123561, #117048, #112998, #14922 ) ) ;
#83847=DIRECTION ( 'NONE',  ( 0.7071067811865487940, -0.7071067811865463515, 0.000000000000000000 ) ) ;
#83848=PLANE ( 'NONE',  #44151 ) ;
#83849=ORIENTED_EDGE ( 'NONE', *, *, #9729, .F. ) ;
#83850=CARTESIAN_POINT ( 'NONE',  ( -23.99999999999983302, 10.55218569542905982, 5.000000000000000000 ) ) ;
#83851=LINE ( 'NONE', #6915, #100494 ) ;
#83852=ORIENTED_EDGE ( 'NONE', *, *, #108336, .F. ) ;
#83854=CARTESIAN_POINT ( 'NONE',  ( 34.92499999999998295, -11.29530194282807365, 17.70209546082494967 ) ) ;
#83856=VECTOR ( 'NONE', #64839, 1000.000000000000000 ) ;
#83857=DIRECTION ( 'NONE',  ( 0.000000000000000000, 0.3543493200069153248, 0.9351131265310291818 ) ) ;
#83858=EDGE_CURVE ( 'NONE', #62399, #11393, #113231, .T. ) ;
#83860=LINE ( 'NONE', #137500, #101891 ) ;
#83862=ORIENTED_EDGE ( 'NONE', *, *, #61906, .T. ) ;
#83863=LINE ( 'NONE', #51930, #141804 ) ;
#83864=ADVANCED_FACE ( 'NONE', ( #103091 ), #100934, .F. ) ;
#83865=LINE ( 'NONE', #51213, #32307 ) ;
#83867=VECTOR ( 'NONE', #27324, 1000.000000000000000 ) ;
#83868=LINE ( 'NONE', #62818, #11974 ) ;
#83872=ORIENTED_EDGE ( 'NONE', *, *, #97259, .T. ) ;
#83875=CARTESIAN_POINT ( 'NONE',  ( -26.99999999999980460, -4.447814304570781196, 5.000000000000000000 ) ) ;
#83877=AXIS2_PLACEMENT_3D ( 'NONE', #37806, #4364, #15276 ) ;
#83878=DIRECTION ( 'NONE',  ( -0.000000000000000000, 0.3543493200069153248, 0.9351131265310292928 ) ) ;
#83879=EDGE_LOOP ( 'NONE', ( #22823, #33263, #103902, #6493 ) ) ;
#83880=DIRECTION ( 'NONE',  ( -0.7071067811865486830, -0.7071067811865464625, 0.000000000000000000 ) ) ;
#83881=CARTESIAN_POINT ( 'NONE',  ( 32.99999999999976552, -1.068876922607802538, 4.000000000000000000 ) ) ;
#83882=DIRECTION ( 'NONE',  ( 0.7071067811865487940, -0.7071067811865463515, 0.000000000000000000 ) ) ;
#83883=EDGE_CURVE ( 'NONE', #127446, #105971, #117501, .T. ) ;
#83884=CARTESIAN_POINT ( 'NONE',  ( -14.54487008052910824, -0.7407075233842735917, 4.335043535661659675 ) ) ;
#83885=EDGE_LOOP ( 'NONE', ( #136130, #110417, #89758, #7846, #109474 ) ) ;
#83886=CARTESIAN_POINT ( 'NONE',  ( 6.489213562373093325, -27.52281430457059841, 5.000000000000000000 ) ) ;
#83887=CARTESIAN_POINT ( 'NONE',  ( -14.11732500641695509, -0.1862019290248694003, 4.000000000000000000 ) ) ;
#83888=VECTOR ( 'NONE', #134307, 1000.000000000000000 ) ;
#83891=ORIENTED_EDGE ( 'NONE', *, *, #49665, .F. ) ;
#83892=EDGE_LOOP ( 'NONE', ( #86533, #136899, #65396, #129210 ) ) ;
#83894=VERTEX_POINT ( 'NONE', #105222 ) ;
#83895=PLANE ( 'NONE',  #5813 ) ;
#83896=DIRECTION ( 'NONE',  ( 0.7071067811865486830, -0.7071067811865464625, -0.000000000000000000 ) ) ;
#83897=DIRECTION ( 'NONE',  ( 0.3543493200069162685, -0.000000000000000000, -0.9351131265310288487 ) ) ;
#83898=ORIENTED_EDGE ( 'NONE', *, *, #81520, .T. ) ;
#83899=AXIS2_PLACEMENT_3D ( 'NONE', #16937, #93783, #60473 ) ;
#83900=AXIS2_PLACEMENT_3D ( 'NONE', #31541, #103533, #42443 ) ;
#83901=VECTOR ( 'NONE', #25203, 999.9999999999998863 ) ;
#83902=CARTESIAN_POINT ( 'NONE',  ( -3.411614905948293863, 22.22500000000000142, 4.777194822843814137 ) ) ;
#83903=CARTESIAN_POINT ( 'NONE',  ( 34.92499999999998295, -6.791953661863733949, 15.99560845316868729 ) ) ;
#83906=VECTOR ( 'NONE', #120979, 1000.000000000000000 ) ;
#83907=EDGE_LOOP ( 'NONE', ( #11720, #53820, #129370, #133942 ) ) ;
#83908=EDGE_CURVE ( 'NONE', #113319, #132165, #6576, .T. ) ;
#83910=CARTESIAN_POINT ( 'NONE',  ( -66.18398860626901126, 28.73617430169833753, 5.000000000000000000 ) ) ;
#83911=VECTOR ( 'NONE', #115365, 1000.000000000000000 ) ;
#83912=CARTESIAN_POINT ( 'NONE',  ( -53.99451991528749062, 28.92564299267975869, 4.000000000000000000 ) ) ;
#83913=FACE_OUTER_BOUND ( 'NONE', #6470, .T. ) ;
#83914=VECTOR ( 'NONE', #49629, 1000.000000000000000 ) ;
#83916=VERTEX_POINT ( 'NONE', #50852 ) ;
#83917=ORIENTED_EDGE ( 'NONE', *, *, #85963, .F. ) ;
#83918=ADVANCED_FACE ( 'NONE', ( #116811 ), #128420, .F. ) ;
#83919=EDGE_CURVE ( 'NONE', #15581, #116374, #93647, .T. ) ;
#83920=CARTESIAN_POINT ( 'NONE',  ( 5.700255128608413102, -27.71228299555201957, 4.000000000000000000 ) ) ;
#83921=DIRECTION ( 'NONE',  ( 0.6830127018922180770, -0.6830127018922204085, -0.2588190451025213501 ) ) ;
#83922=CARTESIAN_POINT ( 'NONE',  ( 38.99451991528749062, 28.92564299267965211, 4.000000000000000000 ) ) ;
#83923=CARTESIAN_POINT ( 'NONE',  ( 0.7928932188134545367, -17.24070752338410628, 5.000000000000000000 ) ) ;
#83925=PLANE ( 'NONE',  #132285 ) ;
#83926=VERTEX_POINT ( 'NONE', #140020 ) ;
#83927=ORIENTED_EDGE ( 'NONE', *, *, #61906, .F. ) ;
#83928=ORIENTED_EDGE ( 'NONE', *, *, #134742, .T. ) ;
#83929=EDGE_LOOP ( 'NONE', ( #140200, #47778, #87332, #42150 ) ) ;
#83930=EDGE_CURVE ( 'NONE', #119756, #121984, #7315, .T. ) ;
#83933=CARTESIAN_POINT ( 'NONE',  ( 20.99999999999985789, -13.97847968911258221, -0.1324546996126314546 ) ) ;
#83934=ORIENTED_EDGE ( 'NONE', *, *, #128759, .F. ) ;
#83935=LINE ( 'NONE', #27350, #41335 ) ;
#83936=CARTESIAN_POINT ( 'NONE',  ( -7.499999999999951150, -4.216083040037264418, -7.486842126848642032 ) ) ;
#83940=AXIS2_PLACEMENT_3D ( 'NONE', #73865, #105742, #106447 ) ;
#83941=FACE_OUTER_BOUND ( 'NONE', #54677, .T. ) ;
#83942=VERTEX_POINT ( 'NONE', #137876 ) ;
#83943=CARTESIAN_POINT ( 'NONE',  ( 66.29974487139159578, -27.71228299555252406, 4.000000000000000000 ) ) ;
#83944=PLANE ( 'NONE',  #122886 ) ;
#83945=ORIENTED_EDGE ( 'NONE', *, *, #52650, .F. ) ;
#83946=CARTESIAN_POINT ( 'NONE',  ( -31.49999999999977973, -6.839392718269155402, -8.480912228396011443 ) ) ;
#83947=EDGE_LOOP ( 'NONE', ( #136213, #93480, #14821, #54676 ) ) ;
#83949=VERTEX_POINT ( 'NONE', #48714 ) ;
#83950=EDGE_LOOP ( 'NONE', ( #12787, #46144, #70646, #108135, #92079 ) ) ;
#83952=EDGE_LOOP ( 'NONE', ( #5056, #38272, #140010, #34727 ) ) ;
#83954=EDGE_CURVE ( 'NONE', #22463, #76469, #92920, .T. ) ;
#83955=DIRECTION ( 'NONE',  ( -0.000000000000000000, 0.000000000000000000, 1.000000000000000000 ) ) ;
#83957=CARTESIAN_POINT ( 'NONE',  ( 7.980122250714476451, -17.24070752338410273, 20.23474786156470984 ) ) ;
#83958=EDGE_CURVE ( 'NONE', #117563, #83102, #86015, .T. ) ;
#83960=CARTESIAN_POINT ( 'NONE',  ( 8.445142094776647568, 22.22500000000000142, -11.43456810075855756 ) ) ;
#83962=DIRECTION ( 'NONE',  ( 0.7071067811865486830, -0.7071067811865464625, -0.000000000000000000 ) ) ;
#83963=VECTOR ( 'NONE', #74399, 1000.000000000000000 ) ;
#83964=CARTESIAN_POINT ( 'NONE',  ( -33.48921356237309510, -27.52281430457078670, 5.000000000000000000 ) ) ;
#83965=EDGE_CURVE ( 'NONE', #81560, #1788, #129113, .T. ) ;
#83966=EDGE_CURVE ( 'NONE', #112039, #118417, #16786, .T. ) ;
#83967=CARTESIAN_POINT ( 'NONE',  ( 24.79289321881329045, -20.24070752338406720, 5.000000000000000000 ) ) ;
#83969=ORIENTED_EDGE ( 'NONE', *, *, #70080, .T. ) ;
#83970=DIRECTION ( 'NONE',  ( 0.7071067811865487940, 0.7071067811865463515, -0.000000000000000000 ) ) ;
#83971=EDGE_LOOP ( 'NONE', ( #112861, #115918, #135658, #41815 ) ) ;
#83972=ORIENTED_EDGE ( 'NONE', *, *, #128746, .F. ) ;
#83975=ORIENTED_EDGE ( 'NONE', *, *, #71713, .T. ) ;
#83976=CARTESIAN_POINT ( 'NONE',  ( -20.91685193227056416, 21.75929247661549226, 7.311836541448005100 ) ) ;
#83977=DIRECTION ( 'NONE',  ( -0.3543493200069162685, -0.000000000000000000, -0.9351131265310288487 ) ) ;
#83979=CARTESIAN_POINT ( 'NONE',  ( -11.81601139373100651, 28.73617430169779041, 5.000000000000000000 ) ) ;
#83981=CARTESIAN_POINT ( 'NONE',  ( 16.40633728939539537, -22.22500000000000142, 24.45136256510390993 ) ) ;
#83982=ORIENTED_EDGE ( 'NONE', *, *, #46314, .F. ) ;
#83985=ORIENTED_EDGE ( 'NONE', *, *, #142388, .F. ) ;
#83986=EDGE_CURVE ( 'NONE', #132252, #33283, #129835, .T. ) ;
#83988=CARTESIAN_POINT ( 'NONE',  ( 23.99999999999985079, 17.96639925780208458, 5.000000000000000000 ) ) ;
#83989=CARTESIAN_POINT ( 'NONE',  ( 4.499999999999972466, -17.56887692260763956, 4.000000000000000000 ) ) ;
#83991=VERTEX_POINT ( 'NONE', #19641 ) ;
#83992=ORIENTED_EDGE ( 'NONE', *, *, #67634, .T. ) ;
#83994=CARTESIAN_POINT ( 'NONE',  ( -59.99451991528749772, 28.92564299267980132, 4.000000000000000000 ) ) ;
#83995=LINE ( 'NONE', #120116, #85727 ) ;
#83996=ADVANCED_FACE ( 'NONE', ( #119638 ), #63884, .F. ) ;
#83997=VECTOR ( 'NONE', #23317, 1000.000000000000000 ) ;
#83998=LINE ( 'NONE', #138347, #100591 ) ;
#83999=AXIS2_PLACEMENT_3D ( 'NONE', #38241, #5580, #30771 ) ;
#84000=LINE ( 'NONE', #17950, #72778 ) ;
#84001=CARTESIAN_POINT ( 'NONE',  ( -29.29289321881324781, 14.25929247661556865, 5.000000000000000000 ) ) ;
#84003=DIRECTION ( 'NONE',  ( 0.7071067811865487940, 0.7071067811865463515, 0.000000000000000000 ) ) ;
#84004=VECTOR ( 'NONE', #29874, 1000.000000000000227 ) ;
#84005=LINE ( 'NONE', #49931, #55585 ) ;
#84006=DIRECTION ( 'NONE',  ( -0.7071067811865487940, 0.7071067811865463515, -0.000000000000000000 ) ) ;
#84007=ORIENTED_EDGE ( 'NONE', *, *, #15900, .F. ) ;
#84009=AXIS2_PLACEMENT_3D ( 'NONE', #140119, #7419, #127073 ) ;
#84010=EDGE_CURVE ( 'NONE', #111700, #122429, #142164, .T. ) ;
#84011=FACE_OUTER_BOUND ( 'NONE', #116100, .T. ) ;
#84012=ORIENTED_EDGE ( 'NONE', *, *, #130289, .F. ) ;
#84013=FACE_OUTER_BOUND ( 'NONE', #46099, .T. ) ;
#84015=VERTEX_POINT ( 'NONE', #52268 ) ;
#84016=DIRECTION ( 'NONE',  ( 0.7071067811865487940, 0.7071067811865463515, 0.000000000000000000 ) ) ;
#84017=ADVANCED_FACE ( 'NONE', ( #74899 ), #42850, .T. ) ;
#84018=LINE ( 'NONE', #128215, #11428 ) ;
#84020=ORIENTED_EDGE ( 'NONE', *, *, #3667, .F. ) ;
#84023=CARTESIAN_POINT ( 'NONE',  ( -27.29974487139158512, -27.71228299555225405, 4.000000000000000000 ) ) ;
#84024=EDGE_CURVE ( 'NONE', #29579, #41631, #43541, .T. ) ;
#84026=DIRECTION ( 'NONE',  ( 0.3543493200069162685, -0.000000000000000000, -0.9351131265310288487 ) ) ;
#84027=AXIS2_PLACEMENT_3D ( 'NONE', #129424, #120678, #108351 ) ;
#84028=PLANE ( 'NONE',  #50593 ) ;
#84029=PLANE ( 'NONE',  #65345 ) ;
#84031=CARTESIAN_POINT ( 'NONE',  ( -2.999999999999975131, -4.068876922607777225, 4.000000000000000000 ) ) ;
#84034=LINE ( 'NONE', #115877, #20460 ) ;
#84035=DIRECTION ( 'NONE',  ( 1.000000000000000000, 0.000000000000000000, 0.000000000000000000 ) ) ;
#84036=CARTESIAN_POINT ( 'NONE',  ( 72.18398860626899705, 28.73617430169837661, 5.000000000000000000 ) ) ;
#84037=VERTEX_POINT ( 'NONE', #87760 ) ;
#84038=VECTOR ( 'NONE', #118860, 1000.000000000000000 ) ;
#84039=VERTEX_POINT ( 'NONE', #121090 ) ;
#84041=DIRECTION ( 'NONE',  ( -1.000000000000000000, 0.000000000000000000, -0.000000000000000000 ) ) ;
#84042=ORIENTED_EDGE ( 'NONE', *, *, #101607, .F. ) ;
#84043=VECTOR ( 'NONE', #117091, 1000.000000000000227 ) ;
#84044=CARTESIAN_POINT ( 'NONE',  ( 15.18398860626900237, 28.73617430169797871, 5.000000000000000000 ) ) ;
#84045=CARTESIAN_POINT ( 'NONE',  ( 56.99451991528749062, 28.92564299267978001, 4.000000000000000000 ) ) ;
#84046=AXIS2_PLACEMENT_3D ( 'NONE', #80316, #124502, #119315 ) ;
#84048=VERTEX_POINT ( 'NONE', #140695 ) ;
#84049=LINE ( 'NONE', #48530, #104163 ) ;
#84050=DIRECTION ( 'NONE',  ( 0.7071067811865487940, -0.7071067811865463515, 0.000000000000000000 ) ) ;
#84051=DIRECTION ( 'NONE',  ( 0.6830127018922181881, 0.6830127018922202975, -0.2588190451025214056 ) ) ;
#84052=LINE ( 'NONE', #99695, #2705 ) ;
#84053=PLANE ( 'NONE',  #81789 ) ;
#84054=DIRECTION ( 'NONE',  ( -0.3543493200069162685, -0.000000000000000000, -0.9351131265310288487 ) ) ;
#84055=CARTESIAN_POINT ( 'NONE',  ( 75.18398860626899705, 28.73617430169839793, 5.000000000000000000 ) ) ;
#84056=DIRECTION ( 'NONE',  ( -0.7071067811865486830, -0.7071067811865464625, 0.000000000000000000 ) ) ;
#84057=LINE ( 'NONE', #52103, #137255 ) ;
#84058=FACE_OUTER_BOUND ( 'NONE', #130456, .T. ) ;
#84059=PLANE ( 'NONE',  #66133 ) ;
#84061=VECTOR ( 'NONE', #78285, 1000.000000000000000 ) ;
#84062=VERTEX_POINT ( 'NONE', #120340 ) ;
#84066=VERTEX_POINT ( 'NONE', #21788 ) ;
#84067=VECTOR ( 'NONE', #98840, 1000.000000000000000 ) ;
#84068=CARTESIAN_POINT ( 'NONE',  ( -51.18398860626899705, 28.73617430169823095, 5.000000000000000000 ) ) ;
#84069=AXIS2_PLACEMENT_3D ( 'NONE', #47174, #21252, #20509 ) ;
#84070=LINE ( 'NONE', #61602, #117191 ) ;
#84071=VERTEX_POINT ( 'NONE', #66037 ) ;
#84073=DIRECTION ( 'NONE',  ( -0.000000000000000000, 0.000000000000000000, 1.000000000000000000 ) ) ;
#84075=ORIENTED_EDGE ( 'NONE', *, *, #94836, .F. ) ;
#84076=LINE ( 'NONE', #63740, #79087 ) ;
#84077=ORIENTED_EDGE ( 'NONE', *, *, #13878, .T. ) ;
#84079=VECTOR ( 'NONE', #85280, 1000.000000000000000 ) ;
#84080=PLANE ( 'NONE',  #21445 ) ;
#84081=CARTESIAN_POINT ( 'NONE',  ( 78.18398860626899705, 28.73617430169841924, 5.000000000000000000 ) ) ;
#84083=EDGE_LOOP ( 'NONE', ( #36203, #105209, #57342, #33442 ) ) ;
#84084=ADVANCED_FACE ( 'NONE', ( #110202 ), #10874, .F. ) ;
#84086=DIRECTION ( 'NONE',  ( -0.6830127018922181881, 0.6830127018922202975, -0.2588190451025214056 ) ) ;
#84087=EDGE_CURVE ( 'NONE', #79941, #18880, #22470, .T. ) ;
#84088=CARTESIAN_POINT ( 'NONE',  ( 51.18398860626899705, 28.73617430169823095, 5.000000000000000000 ) ) ;
#84090=VECTOR ( 'NONE', #96283, 1000.000000000000000 ) ;
#84091=DIRECTION ( 'NONE',  ( 0.3543493200069162685, -0.000000000000000000, -0.9351131265310288487 ) ) ;
#84095=CARTESIAN_POINT ( 'NONE',  ( -60.48921356237309510, -27.52281430457097500, 5.000000000000000000 ) ) ;
#84096=ORIENTED_EDGE ( 'NONE', *, *, #45542, .T. ) ;
#84097=ORIENTED_EDGE ( 'NONE', *, *, #7625, .T. ) ;
#84098=AXIS2_PLACEMENT_3D ( 'NONE', #99273, #142807, #109465 ) ;
#84100=EDGE_CURVE ( 'NONE', #66103, #62418, #75864, .T. ) ;
#84102=CARTESIAN_POINT ( 'NONE',  ( 71.99451991528749772, 28.92564299267988304, 4.000000000000000000 ) ) ;
#84103=CARTESIAN_POINT ( 'NONE',  ( 21.79289321881330821, 15.75929247661555799, 5.000000000000000000 ) ) ;
#84104=EDGE_LOOP ( 'NONE', ( #20946, #83507, #6894, #133832 ) ) ;
#84105=CARTESIAN_POINT ( 'NONE',  ( -5.018447346356667893, 18.75929247661552424, 20.33588619593443880 ) ) ;
#84106=CARTESIAN_POINT ( 'NONE',  ( 60.18398860626900415, 28.73617430169829490, 5.000000000000000000 ) ) ;
#84107=VECTOR ( 'NONE', #9838, 1000.000000000000000 ) ;
#84108=CARTESIAN_POINT ( 'NONE',  ( 32.99999999999976552, 15.45873954670188155, -0.03131636524301723706 ) ) ;
#84109=EDGE_CURVE ( 'NONE', #55527, #84757, #95320, .T. ) ;
#84110=CARTESIAN_POINT ( 'NONE',  ( -41.99451991528749062, 28.92564299267967343, 4.000000000000000000 ) ) ;
#84111=ORIENTED_EDGE ( 'NONE', *, *, #50421, .F. ) ;
#84112=CARTESIAN_POINT ( 'NONE',  ( 10.49999999999992539, 18.05218569542898521, 5.000000000000000000 ) ) ;
#84115=CARTESIAN_POINT ( 'NONE',  ( 8.999999999999934275, 7.588810512006216591, -3.013526669885247866 ) ) ;
#84116=LINE ( 'NONE', #92802, #89691 ) ;
#84117=VERTEX_POINT ( 'NONE', #11588 ) ;
#84118=DIRECTION ( 'NONE',  ( 0.7071067811865487940, -0.7071067811865463515, 0.000000000000000000 ) ) ;
#84119=ORIENTED_EDGE ( 'NONE', *, *, #129757, .F. ) ;
#84120=ORIENTED_EDGE ( 'NONE', *, *, #93584, .F. ) ;
#84121=ORIENTED_EDGE ( 'NONE', *, *, #5818, .T. ) ;
#84123=VECTOR ( 'NONE', #56024, 1000.000000000000000 ) ;
#84124=CARTESIAN_POINT ( 'NONE',  ( -4.828169399223495084, -2.240707523384262601, 4.000000000000000000 ) ) ;
#84126=CARTESIAN_POINT ( 'NONE',  ( -34.42500000000001137, -3.022814304570547783, 5.000000000000000000 ) ) ;
#84127=DIRECTION ( 'NONE',  ( 0.7071067811865486830, -0.7071067811865464625, -0.000000000000000000 ) ) ;
#84128=EDGE_CURVE ( 'NONE', #27164, #84039, #90631, .T. ) ;
#84129=LINE ( 'NONE', #63791, #94483 ) ;
#84130=FACE_OUTER_BOUND ( 'NONE', #99026, .T. ) ;
#84131=AXIS2_PLACEMENT_3D ( 'NONE', #42599, #131016, #76648 ) ;
#84132=DIRECTION ( 'NONE',  ( -0.7071067811865486830, -0.7071067811865464625, 0.000000000000000000 ) ) ;
#84133=ADVANCED_FACE ( 'NONE', ( #56612 ), #2130, .T. ) ;
#84134=ADVANCED_FACE ( 'NONE', ( #133420 ), #2877, .F. ) ;
#84135=FACE_OUTER_BOUND ( 'NONE', #65802, .T. ) ;
#84136=CARTESIAN_POINT ( 'NONE',  ( -10.49999999999993960, 16.08746187583909659, 4.000000000000000000 ) ) ;
#84137=AXIS2_PLACEMENT_3D ( 'NONE', #117611, #16913, #114763 ) ;
#84138=DIRECTION ( 'NONE',  ( 0.7071067811865487940, 0.7071067811865463515, 0.000000000000000000 ) ) ;
#84140=ORIENTED_EDGE ( 'NONE', *, *, #36190, .T. ) ;
#84141=EDGE_LOOP ( 'NONE', ( #30676, #106675, #65919, #20103 ) ) ;
#84142=ORIENTED_EDGE ( 'NONE', *, *, #132746, .T. ) ;
#84145=EDGE_CURVE ( 'NONE', #84071, #116810, #13734, .T. ) ;
#84146=VECTOR ( 'NONE', #111971, 1000.000000000000000 ) ;
#84147=EDGE_LOOP ( 'NONE', ( #58752, #102679, #102723, #9366 ) ) ;
#84148=CARTESIAN_POINT ( 'NONE',  ( 0.000000000000000000, 0.000000000000000000, 5.000000000000000000 ) ) ;
#84149=ADVANCED_FACE ( 'NONE', ( #36245 ), #89887, .F. ) ;
#84151=CARTESIAN_POINT ( 'NONE',  ( 18.48921356237309510, -27.52281430457068367, 5.000000000000000000 ) ) ;
#84152=ORIENTED_EDGE ( 'NONE', *, *, #87190, .T. ) ;
#84153=CARTESIAN_POINT ( 'NONE',  ( -42.18398860626899705, 28.73617430169816700, 5.000000000000000000 ) ) ;
#84154=EDGE_LOOP ( 'NONE', ( #8856, #82360, #63987, #124230 ) ) ;
#84155=LINE ( 'NONE', #72585, #123107 ) ;
#84156=VECTOR ( 'NONE', #79501, 1000.000000000000114 ) ;
#84157=DIRECTION ( 'NONE',  ( -0.000000000000000000, 0.3543493200069153248, 0.9351131265310292928 ) ) ;
#84158=VECTOR ( 'NONE', #51164, 999.9999999999998863 ) ;
#84163=LINE ( 'NONE', #139249, #4978 ) ;
#84164=LINE ( 'NONE', #38490, #120569 ) ;
#84165=ORIENTED_EDGE ( 'NONE', *, *, #64862, .T. ) ;
#84166=EDGE_LOOP ( 'NONE', ( #93104, #102731, #87907, #71807 ) ) ;
#84167=FACE_OUTER_BOUND ( 'NONE', #44760, .T. ) ;
#84168=ORIENTED_EDGE ( 'NONE', *, *, #14513, .T. ) ;
#84170=AXIS2_PLACEMENT_3D ( 'NONE', #115005, #93993, #47694 ) ;
#84171=CARTESIAN_POINT ( 'NONE',  ( -12.85181644961847169, 17.25929247661554555, 8.802941693769172460 ) ) ;
#84173=EDGE_CURVE ( 'NONE', #98151, #13095, #6471, .T. ) ;
#84174=DIRECTION ( 'NONE',  ( -0.3543493200069162685, -0.000000000000000000, -0.9351131265310288487 ) ) ;
#84177=DIRECTION ( 'NONE',  ( 0.3543493200069162685, -0.000000000000000000, -0.9351131265310288487 ) ) ;
#84178=LINE ( 'NONE', #73285, #74375 ) ;
#84179=DIRECTION ( 'NONE',  ( -0.6830127018922180770, -0.6830127018922204085, -0.2588190451025213501 ) ) ;
#84180=ORIENTED_EDGE ( 'NONE', *, *, #102441, .T. ) ;
#84182=AXIS2_PLACEMENT_3D ( 'NONE', #37084, #47315, #47996 ) ;
#84183=LINE ( 'NONE', #73289, #102611 ) ;
#84184=VERTEX_POINT ( 'NONE', #84802 ) ;
#84186=ORIENTED_EDGE ( 'NONE', *, *, #134515, .F. ) ;
#84187=ORIENTED_EDGE ( 'NONE', *, *, #89638, .F. ) ;
#84188=DIRECTION ( 'NONE',  ( -0.000000000000000000, -0.3543493200069152693, 0.9351131265310292928 ) ) ;
#84189=LINE ( 'NONE', #30499, #143298 ) ;
#84190=ORIENTED_EDGE ( 'NONE', *, *, #142424, .T. ) ;
#84191=LINE ( 'NONE', #117467, #55863 ) ;
#84192=ADVANCED_FACE ( 'NONE', ( #96351 ), #129012, .F. ) ;
#84194=ADVANCED_FACE ( 'NONE', ( #63083 ), #7930, .T. ) ;
#84195=CARTESIAN_POINT ( 'NONE',  ( 27.18398860626900060, 28.73617430169806042, 5.000000000000000000 ) ) ;
#84196=VECTOR ( 'NONE', #33845, 1000.000000000000000 ) ;
#84197=DIRECTION ( 'NONE',  ( -0.6830127018922180770, -0.6830127018922204085, -0.2588190451025213501 ) ) ;
#84198=CARTESIAN_POINT ( 'NONE',  ( -29.29289321881324426, 17.25929247661553845, 5.000000000000000000 ) ) ;
#84199=LINE ( 'NONE', #58904, #99974 ) ;
#84200=DIRECTION ( 'NONE',  ( 0.7071067811865486830, -0.7071067811865464625, -0.000000000000000000 ) ) ;
#84201=CARTESIAN_POINT ( 'NONE',  ( 29.99999999999979039, 19.93112307739198386, 4.000000000000000000 ) ) ;
#84202=CARTESIAN_POINT ( 'NONE',  ( -24.29974487139158867, -27.71228299555223273, 4.000000000000000000 ) ) ;
#84203=CARTESIAN_POINT ( 'NONE',  ( 20.99999999999985079, 8.816494571476654940, 4.604407763760433703 ) ) ;
#84204=FACE_OUTER_BOUND ( 'NONE', #141522, .T. ) ;
#84206=ORIENTED_EDGE ( 'NONE', *, *, #132773, .T. ) ;
#84207=VECTOR ( 'NONE', #112951, 999.9999999999998863 ) ;
#84208=ORIENTED_EDGE ( 'NONE', *, *, #108598, .F. ) ;
#84211=ORIENTED_EDGE ( 'NONE', *, *, #86079, .T. ) ;
#84213=EDGE_LOOP ( 'NONE', ( #49268, #17563, #128967, #132422 ) ) ;
#84214=LINE ( 'NONE', #128410, #36366 ) ;
#84215=FACE_OUTER_BOUND ( 'NONE', #57397, .T. ) ;
#84217=ORIENTED_EDGE ( 'NONE', *, *, #96901, .F. ) ;
#84218=DIRECTION ( 'NONE',  ( -0.6830127018922181881, 0.6830127018922202975, -0.2588190451025214056 ) ) ;
#84219=DIRECTION ( 'NONE',  ( -0.7071067811865486830, -0.7071067811865464625, -0.000000000000000000 ) ) ;
#84220=DIRECTION ( 'NONE',  ( 0.7071067811865486830, -0.7071067811865464625, -0.000000000000000000 ) ) ;
#84221=LINE ( 'NONE', #75465, #99778 ) ;
#84223=VERTEX_POINT ( 'NONE', #97816 ) ;
#84224=DIRECTION ( 'NONE',  ( 1.000000000000000000, -0.000000000000000000, -0.000000000000000000 ) ) ;
#84225=CARTESIAN_POINT ( 'NONE',  ( 32.67183060077623935, 11.25929247661559884, 4.000000000000000000 ) ) ;
#84226=CARTESIAN_POINT ( 'NONE',  ( -24.71757738642550351, -21.73023691814493219, 5.000000000000000888 ) ) ;
#84227=LINE ( 'NONE', #20877, #72957 ) ;
#84228=VECTOR ( 'NONE', #128143, 1000.000000000000000 ) ;
#84229=CARTESIAN_POINT ( 'NONE',  ( -32.99999999999976552, 8.966399257802180500, 5.000000000000000000 ) ) ;
#84230=CARTESIAN_POINT ( 'NONE',  ( -9.707106781186476852, 2.259292476615701428, 5.000000000000000000 ) ) ;
#84233=VECTOR ( 'NONE', #39982, 1000.000000000000000 ) ;
#84235=EDGE_LOOP ( 'NONE', ( #23447, #23761, #73346, #138504 ) ) ;
#84236=ORIENTED_EDGE ( 'NONE', *, *, #14347, .T. ) ;
#84238=ORIENTED_EDGE ( 'NONE', *, *, #107722, .F. ) ;
#84239=CARTESIAN_POINT ( 'NONE',  ( -11.99451991528749417, 28.92564299267946382, 4.000000000000000000 ) ) ;
#84240=EDGE_CURVE ( 'NONE', #98041, #105535, #54352, .T. ) ;
#84241=CARTESIAN_POINT ( 'NONE',  ( -60.18398860626900415, 28.73617430169829490, 5.000000000000000000 ) ) ;
#84243=VECTOR ( 'NONE', #74144, 1000.000000000000000 ) ;
#84244=LINE ( 'NONE', #84923, #37371 ) ;
#84245=LINE ( 'NONE', #126984, #58161 ) ;
#84247=VECTOR ( 'NONE', #17440, 1000.000000000000000 ) ;
#84248=ORIENTED_EDGE ( 'NONE', *, *, #42528, .T. ) ;
#84250=ORIENTED_EDGE ( 'NONE', *, *, #10713, .T. ) ;
#84251=DIRECTION ( 'NONE',  ( -0.7071067811865486830, -0.7071067811865464625, 0.000000000000000000 ) ) ;
#84252=CARTESIAN_POINT ( 'NONE',  ( 57.48921356237308800, -27.52281430457095368, 5.000000000000000000 ) ) ;
#84253=CARTESIAN_POINT ( 'NONE',  ( -32.29298673570672662, -21.74070752338405299, 4.999753212805210012 ) ) ;
#84254=ADVANCED_FACE ( 'NONE', ( #44169 ), #89788, .T. ) ;
#84255=FACE_OUTER_BOUND ( 'NONE', #90519, .T. ) ;
#84256=ORIENTED_EDGE ( 'NONE', *, *, #99142, .F. ) ;
#84258=EDGE_CURVE ( 'NONE', #125811, #142084, #23075, .T. ) ;
#84259=ORIENTED_EDGE ( 'NONE', *, *, #109081, .F. ) ;
#84260=LINE ( 'NONE', #93684, #49448 ) ;
#84261=CARTESIAN_POINT ( 'NONE',  ( 27.48921356237309155, -27.52281430457074762, 5.000000000000000000 ) ) ;
#84262=CARTESIAN_POINT ( 'NONE',  ( 57.18398860626899705, 28.73617430169827358, 5.000000000000000000 ) ) ;
#84263=CARTESIAN_POINT ( 'NONE',  ( 32.22995720542186149, 21.73644205237997440, 5.000000000000000888 ) ) ;
#84265=AXIS2_PLACEMENT_3D ( 'NONE', #30042, #74293, #86602 ) ;
#84266=EDGE_CURVE ( 'NONE', #30354, #120324, #121690, .T. ) ;
#84267=ADVANCED_FACE ( 'NONE', ( #65941 ), #110802, .F. ) ;
#84268=AXIS2_PLACEMENT_3D ( 'NONE', #9356, #119555, #51495 ) ;
#84270=ORIENTED_EDGE ( 'NONE', *, *, #88127, .F. ) ;
#84271=DIRECTION ( 'NONE',  ( -0.000000000000000000, 0.3543493200069153248, 0.9351131265310292928 ) ) ;
#84273=DIRECTION ( 'NONE',  ( -0.000000000000000000, -0.3543493200069152693, 0.9351131265310292928 ) ) ;
#84274=ORIENTED_EDGE ( 'NONE', *, *, #70036, .T. ) ;
#84275=VERTEX_POINT ( 'NONE', #143453 ) ;
#84276=VECTOR ( 'NONE', #14039, 1000.000000000000227 ) ;
#84277=VERTEX_POINT ( 'NONE', #131161 ) ;
#84278=ADVANCED_FACE ( 'NONE', ( #12221 ), #10777, .F. ) ;
#84280=ORIENTED_EDGE ( 'NONE', *, *, #11423, .T. ) ;
#84282=EDGE_CURVE ( 'NONE', #98856, #59256, #31852, .T. ) ;
#84283=VECTOR ( 'NONE', #32996, 1000.000000000000000 ) ;
#84284=EDGE_CURVE ( 'NONE', #57178, #51263, #76071, .T. ) ;
#84285=FACE_BOUND ( 'NONE', #139330, .T. ) ;
#84287=DIRECTION ( 'NONE',  ( 0.6830127018922181881, 0.6830127018922202975, -0.2588190451025214056 ) ) ;
#84288=DIRECTION ( 'NONE',  ( 0.6830127018922181881, 0.6830127018922202975, -0.2588190451025214056 ) ) ;
#84289=ORIENTED_EDGE ( 'NONE', *, *, #65669, .T. ) ;
#84291=ORIENTED_EDGE ( 'NONE', *, *, #45609, .F. ) ;
#84292=ADVANCED_FACE ( 'NONE', ( #120238 ), #20957, .F. ) ;
#84293=ORIENTED_EDGE ( 'NONE', *, *, #42419, .F. ) ;
#84294=CARTESIAN_POINT ( 'NONE',  ( 26.99451991528749417, 28.92564299267956685, 4.000000000000000000 ) ) ;
#84297=AXIS2_PLACEMENT_3D ( 'NONE', #70611, #69894, #72764 ) ;
#84298=VERTEX_POINT ( 'NONE', #10084 ) ;
#84299=FACE_OUTER_BOUND ( 'NONE', #40128, .T. ) ;
#84300=CARTESIAN_POINT ( 'NONE',  ( 2.999999999999981792, 1.761378380278684430, -6.096875308897248935 ) ) ;
#84301=EDGE_CURVE ( 'NONE', #59037, #4133, #99214, .T. ) ;
#84302=EDGE_LOOP ( 'NONE', ( #134324, #122605, #57368, #41515 ) ) ;
#84303=LINE ( 'NONE', #50939, #51441 ) ;
#84304=VECTOR ( 'NONE', #47246, 999.9999999999998863 ) ;
#84305=ADVANCED_FACE ( 'NONE', ( #98527 ), #87657, .F. ) ;
#84307=FACE_OUTER_BOUND ( 'NONE', #140554, .T. ) ;
#84309=EDGE_CURVE ( 'NONE', #141405, #76093, #89103, .T. ) ;
#84310=DIRECTION ( 'NONE',  ( -0.7071067811865487940, 0.7071067811865463515, 0.000000000000000000 ) ) ;
#84311=DIRECTION ( 'NONE',  ( -0.6830127018922180770, -0.6830127018922204085, -0.2588190451025213501 ) ) ;
#84312=EDGE_LOOP ( 'NONE', ( #141571, #63271, #98421, #90326 ) ) ;
#84313=ORIENTED_EDGE ( 'NONE', *, *, #62500, .T. ) ;
#84314=PLANE ( 'NONE',  #63624 ) ;
#84316=ORIENTED_EDGE ( 'NONE', *, *, #131399, .F. ) ;
#84317=EDGE_CURVE ( 'NONE', #122980, #67467, #34005, .T. ) ;
#84318=ORIENTED_EDGE ( 'NONE', *, *, #52306, .T. ) ;
#84320=DIRECTION ( 'NONE',  ( -0.3543493200069163240, 0.000000000000000000, -0.9351131265310288487 ) ) ;
#84321=CARTESIAN_POINT ( 'NONE',  ( -2.816011393730999401, 28.73617430169785436, 5.000000000000000000 ) ) ;
#84322=ORIENTED_EDGE ( 'NONE', *, *, #4635, .T. ) ;
#84323=DIRECTION ( 'NONE',  ( -0.7071067811865486830, -0.7071067811865464625, 0.000000000000000000 ) ) ;
#84324=AXIS2_PLACEMENT_3D ( 'NONE', #48251, #60601, #80897 ) ;
#84325=FACE_OUTER_BOUND ( 'NONE', #3628, .T. ) ;
#84326=VECTOR ( 'NONE', #70144, 1000.000000000000000 ) ;
#84328=DIRECTION ( 'NONE',  ( 0.7071067811865487940, -0.7071067811865463515, 0.000000000000000000 ) ) ;
#84329=VERTEX_POINT ( 'NONE', #100686 ) ;
#84330=FACE_OUTER_BOUND ( 'NONE', #28053, .T. ) ;
#84331=ADVANCED_FACE ( 'NONE', ( #1333 ), #134029, .F. ) ;
#84332=CARTESIAN_POINT ( 'NONE',  ( 27.29974487139158512, -27.71228299555225405, 4.000000000000000000 ) ) ;
#84333=LINE ( 'NONE', #117602, #54244 ) ;
#84334=CARTESIAN_POINT ( 'NONE',  ( 11.67183060077638501, 2.259292476615694323, 4.000000000000000000 ) ) ;
#84335=ORIENTED_EDGE ( 'NONE', *, *, #8978, .F. ) ;
#84336=CARTESIAN_POINT ( 'NONE',  ( 5.683420388672068668, -6.740707523384219968, 11.88629033278122726 ) ) ;
#84337=ORIENTED_EDGE ( 'NONE', *, *, #59368, .T. ) ;
#84339=EDGE_CURVE ( 'NONE', #86087, #3663, #124571, .T. ) ;
#84340=LINE ( 'NONE', #106024, #93277 ) ;
#84341=DIRECTION ( 'NONE',  ( 0.6830127018922181881, 0.6830127018922202975, -0.2588190451025214056 ) ) ;
#84342=ORIENTED_EDGE ( 'NONE', *, *, #103620, .T. ) ;
#84343=AXIS2_PLACEMENT_3D ( 'NONE', #58705, #115121, #137647 ) ;
#84344=VECTOR ( 'NONE', #70540, 1000.000000000000000 ) ;
#84345=PLANE ( 'NONE',  #54174 ) ;
#84346=LINE ( 'NONE', #71312, #10 ) ;
#84347=CARTESIAN_POINT ( 'NONE',  ( 0.000000000000000000, 0.000000000000000000, 5.000000000000000000 ) ) ;
#84348=ORIENTED_EDGE ( 'NONE', *, *, #141064, .F. ) ;
#84349=CARTESIAN_POINT ( 'NONE',  ( 27.48921356237309155, -27.52281430457074762, 5.000000000000000000 ) ) ;
#84350=PLANE ( 'NONE',  #16852 ) ;
#84352=CARTESIAN_POINT ( 'NONE',  ( -15.13499573751613347, 3.759292476615671230, 15.36553568819729421 ) ) ;
#84353=CARTESIAN_POINT ( 'NONE',  ( -22.45764329680115878, -1.725981765586489525, 4.380536896699288363 ) ) ;
#84354=CARTESIAN_POINT ( 'NONE',  ( -13.49999999999992184, -14.70932175296479549, -11.46312253303834616 ) ) ;
#84357=EDGE_CURVE ( 'NONE', #83610, #87604, #49173, .T. ) ;
#84358=ORIENTED_EDGE ( 'NONE', *, *, #112390, .F. ) ;
#84359=DIRECTION ( 'NONE',  ( 0.7071067811865487940, 0.7071067811865463515, 0.000000000000000000 ) ) ;
#84360=LINE ( 'NONE', #61884, #103844 ) ;
#84361=VECTOR ( 'NONE', #127414, 1000.000000000000000 ) ;
#84363=FACE_OUTER_BOUND ( 'NONE', #60061, .T. ) ;
#84364=VECTOR ( 'NONE', #106023, 1000.000000000000000 ) ;
#84365=LINE ( 'NONE', #126396, #115413 ) ;
#84366=CARTESIAN_POINT ( 'NONE',  ( 0.000000000000000000, 0.000000000000000000, 5.000000000000000000 ) ) ;
#84367=ORIENTED_EDGE ( 'NONE', *, *, #21178, .T. ) ;
#84369=CARTESIAN_POINT ( 'NONE',  ( 36.09667064187383545, -2.240707523384260824, 15.26439735382760787 ) ) ;
#84370=CARTESIAN_POINT ( 'NONE',  ( 56.99451991528749062, 28.92564299267978001, 4.000000000000000000 ) ) ;
#84371=CARTESIAN_POINT ( 'NONE',  ( 0.000000000000000000, 0.000000000000000000, 5.000000000000000000 ) ) ;
#84373=DIRECTION ( 'NONE',  ( 0.7071067811865487940, 0.7071067811865463515, -0.000000000000000000 ) ) ;
#84374=EDGE_CURVE ( 'NONE', #65716, #54738, #47762, .T. ) ;
#84375=ORIENTED_EDGE ( 'NONE', *, *, #54646, .T. ) ;
#84376=LINE ( 'NONE', #74924, #18597 ) ;
#84377=ORIENTED_EDGE ( 'NONE', *, *, #105076, .F. ) ;
#84378=EDGE_LOOP ( 'NONE', ( #118876, #87509, #135368, #15176, #115972 ) ) ;
#84379=DIRECTION ( 'NONE',  ( -0.7071067811865486830, -0.7071067811865464625, -0.000000000000000000 ) ) ;
#84381=CARTESIAN_POINT ( 'NONE',  ( -29.67183060077626422, 5.259292476615659240, 4.000000000000000000 ) ) ;
#84382=DIRECTION ( 'NONE',  ( 0.7071067811865487940, 0.7071067811865463515, 0.000000000000000000 ) ) ;
#84384=CARTESIAN_POINT ( 'NONE',  ( -33.18398860626899705, 28.73617430169810305, 5.000000000000000000 ) ) ;
#84385=CARTESIAN_POINT ( 'NONE',  ( 19.49999999999988276, 19.08746187583905041, 4.000000000000000000 ) ) ;
#84387=PLANE ( 'NONE',  #18579 ) ;
#84389=LINE ( 'NONE', #118397, #100545 ) ;
#84390=LINE ( 'NONE', #17648, #4479 ) ;
#84391=PLANE ( 'NONE',  #93719 ) ;
#84392=PLANE ( 'NONE',  #87417 ) ;
#84395=VERTEX_POINT ( 'NONE', #25245 ) ;
#84396=ORIENTED_EDGE ( 'NONE', *, *, #122794, .F. ) ;
#84398=LINE ( 'NONE', #8199, #37796 ) ;
#84399=PLANE ( 'NONE',  #41596 ) ;
#84400=VERTEX_POINT ( 'NONE', #4877 ) ;
#84401=VECTOR ( 'NONE', #41288, 1000.000000000000227 ) ;
#84402=FACE_OUTER_BOUND ( 'NONE', #34738, .T. ) ;
#84403=ADVANCED_FACE ( 'NONE', ( #104209 ), #137598, .F. ) ;
#84405=EDGE_LOOP ( 'NONE', ( #140683, #100135, #36927, #88092 ) ) ;
#84406=EDGE_CURVE ( 'NONE', #86990, #50436, #48436, .T. ) ;
#84407=CARTESIAN_POINT ( 'NONE',  ( -54.29974487139159578, -27.71228299555243879, 4.000000000000000000 ) ) ;
#84408=ORIENTED_EDGE ( 'NONE', *, *, #24451, .T. ) ;
#84409=VERTEX_POINT ( 'NONE', #36837 ) ;
#84410=DIRECTION ( 'NONE',  ( -0.7071067811865486830, -0.7071067811865464625, 0.000000000000000000 ) ) ;
#84411=LINE ( 'NONE', #94526, #47734 ) ;
#84412=CARTESIAN_POINT ( 'NONE',  ( -36.29974487139159578, -27.71228299555231445, 4.000000000000000000 ) ) ;
#84413=LINE ( 'NONE', #137356, #104158 ) ;
#84414=CARTESIAN_POINT ( 'NONE',  ( 34.92499999999998295, 22.22500000000000142, 4.000000000000000000 ) ) ;
#84415=EDGE_CURVE ( 'NONE', #135826, #108262, #58663, .T. ) ;
#84416=EDGE_CURVE ( 'NONE', #83894, #12991, #119426, .T. ) ;
#84417=FACE_OUTER_BOUND ( 'NONE', #93733, .T. ) ;
#84420=CARTESIAN_POINT ( 'NONE',  ( -29.48334561358934991, 22.22500000000000142, 4.500000000000000888 ) ) ;
#84421=LINE ( 'NONE', #70698, #137362 ) ;
#84422=VECTOR ( 'NONE', #121876, 1000.000000000000000 ) ;
#84423=DIRECTION ( 'NONE',  ( -0.3543493200069162685, -0.000000000000000000, -0.9351131265310288487 ) ) ;
#84425=ORIENTED_EDGE ( 'NONE', *, *, #74291, .T. ) ;
#84426=EDGE_CURVE ( 'NONE', #120806, #89946, #46337, .T. ) ;
#84427=VECTOR ( 'NONE', #74035, 1000.000000000000000 ) ;
#84429=EDGE_CURVE ( 'NONE', #46897, #84117, #125287, .T. ) ;
#84432=VECTOR ( 'NONE', #29964, 1000.000000000000000 ) ;
#84433=CARTESIAN_POINT ( 'NONE',  ( -28.82816939922332011, 21.75929247661549937, 4.000000000000000000 ) ) ;
#84434=EDGE_CURVE ( 'NONE', #139479, #21681, #136868, .T. ) ;
#84435=FACE_OUTER_BOUND ( 'NONE', #8671, .T. ) ;
#84436=VERTEX_POINT ( 'NONE', #37576 ) ;
#84437=ORIENTED_EDGE ( 'NONE', *, *, #139235, .F. ) ;
#84439=PLANE ( 'NONE',  #42246 ) ;
#84440=LINE ( 'NONE', #103288, #7375 ) ;
#84441=VERTEX_POINT ( 'NONE', #94770 ) ;
#84442=EDGE_CURVE ( 'NONE', #10011, #4056, #128157, .T. ) ;
#84444=DIRECTION ( 'NONE',  ( -0.000000000000000000, 0.000000000000000000, 1.000000000000000000 ) ) ;
#84445=ORIENTED_EDGE ( 'NONE', *, *, #101893, .F. ) ;
#84446=DIRECTION ( 'NONE',  ( 0.6830127018922181881, 0.6830127018922202975, -0.2588190451025214056 ) ) ;
#84447=EDGE_CURVE ( 'NONE', #94939, #84223, #28114, .T. ) ;
#84448=FACE_BOUND ( 'NONE', #97973, .T. ) ;
#84449=CARTESIAN_POINT ( 'NONE',  ( 0.000000000000000000, 0.000000000000000000, 5.000000000000000000 ) ) ;
#84451=CARTESIAN_POINT ( 'NONE',  ( 51.29974487139158867, -27.71228299555242103, 4.000000000000000000 ) ) ;
#84452=CARTESIAN_POINT ( 'NONE',  ( -12.48921356237309155, -27.52281430457064104, 5.000000000000000000 ) ) ;
#84453=ORIENTED_EDGE ( 'NONE', *, *, #102751, .T. ) ;
#84454=ADVANCED_FACE ( 'NONE', ( #139023 ), #51305, .T. ) ;
#84455=VECTOR ( 'NONE', #19231, 1000.000000000000000 ) ;
#84456=ORIENTED_EDGE ( 'NONE', *, *, #121223, .F. ) ;
#84457=VECTOR ( 'NONE', #122373, 1000.000000000000000 ) ;
#84458=VECTOR ( 'NONE', #65988, 1000.000000000000000 ) ;
#84459=ORIENTED_EDGE ( 'NONE', *, *, #52715, .F. ) ;
#84461=VERTEX_POINT ( 'NONE', #85326 ) ;
#84462=AXIS2_PLACEMENT_3D ( 'NONE', #142043, #8590, #133304 ) ;
#84463=DIRECTION ( 'NONE',  ( -0.000000000000000000, -0.3543493200069152693, 0.9351131265310292928 ) ) ;
#84464=CARTESIAN_POINT ( 'NONE',  ( -29.99999999999978684, -7.447814304570752775, 5.000000000000000000 ) ) ;
#84465=DIRECTION ( 'NONE',  ( 0.6830127018922181881, 0.6830127018922202975, -0.2588190451025214056 ) ) ;
#84466=DIRECTION ( 'NONE',  ( 0.6830127018922180770, -0.6830127018922204085, -0.2588190451025213501 ) ) ;
#84467=EDGE_CURVE ( 'NONE', #94978, #109375, #129549, .T. ) ;
#84468=ORIENTED_EDGE ( 'NONE', *, *, #41673, .T. ) ;
#84469=PLANE ( 'NONE',  #96979 ) ;
#84471=FACE_OUTER_BOUND ( 'NONE', #110815, .T. ) ;
#84472=EDGE_CURVE ( 'NONE', #136324, #30765, #117933, .T. ) ;
#84473=CARTESIAN_POINT ( 'NONE',  ( 5.999999999999970690, 2.587461875839214720, 4.000000000000000000 ) ) ;
#84474=CARTESIAN_POINT ( 'NONE',  ( -14.99999999999989342, -3.412538124160717778, 4.000000000000000000 ) ) ;
#84476=EDGE_LOOP ( 'NONE', ( #113919, #10151, #39564, #61054 ) ) ;
#84477=CARTESIAN_POINT ( 'NONE',  ( 27.48921356237309155, -27.52281430457074762, 5.000000000000000000 ) ) ;
#84479=DIRECTION ( 'NONE',  ( 0.3543493200069162685, -0.000000000000000000, -0.9351131265310288487 ) ) ;
#84480=EDGE_LOOP ( 'NONE', ( #46741, #63216, #33668, #73774, #107196 ) ) ;
#84481=EDGE_LOOP ( 'NONE', ( #423, #24087, #129927, #43298 ) ) ;
#84482=ORIENTED_EDGE ( 'NONE', *, *, #66863, .F. ) ;
#84487=ORIENTED_EDGE ( 'NONE', *, *, #122710, .T. ) ;
#84489=CARTESIAN_POINT ( 'NONE',  ( 57.18398860626899705, 28.73617430169827358, 5.000000000000000000 ) ) ;
#84490=ORIENTED_EDGE ( 'NONE', *, *, #54093, .F. ) ;
#84491=CARTESIAN_POINT ( 'NONE',  ( -47.99451991528749062, 28.92564299267971251, 4.000000000000000000 ) ) ;
#84493=FACE_OUTER_BOUND ( 'NONE', #56623, .T. ) ;
#84495=ORIENTED_EDGE ( 'NONE', *, *, #20065, .T. ) ;
#84496=VECTOR ( 'NONE', #16684, 999.9999999999998863 ) ;
#84497=CARTESIAN_POINT ( 'NONE',  ( 11.67183060077639212, 14.25929247661557753, 4.000000000000000000 ) ) ;
#84498=ORIENTED_EDGE ( 'NONE', *, *, #80962, .T. ) ;
#84499=LINE ( 'NONE', #75758, #59695 ) ;
#84500=ORIENTED_EDGE ( 'NONE', *, *, #61599, .F. ) ;
#84501=ORIENTED_EDGE ( 'NONE', *, *, #19337, .F. ) ;
#84502=ADVANCED_FACE ( 'NONE', ( #127413 ), #38987, .F. ) ;
#84503=VERTEX_POINT ( 'NONE', #7761 ) ;
#84504=VERTEX_POINT ( 'NONE', #116547 ) ;
#84505=DIRECTION ( 'NONE',  ( -0.6830127018922181881, 0.6830127018922202975, -0.2588190451025214056 ) ) ;
#84506=LINE ( 'NONE', #38844, #84043 ) ;
#84508=EDGE_CURVE ( 'NONE', #141704, #94354, #52010, .T. ) ;
#84509=CARTESIAN_POINT ( 'NONE',  ( -5.999999999999963585, 1.761378380278677547, -6.096875308897267587 ) ) ;
#84510=ORIENTED_EDGE ( 'NONE', *, *, #118077, .T. ) ;
#84512=ADVANCED_FACE ( 'NONE', ( #5615 ), #105640, .F. ) ;
#84513=VERTEX_POINT ( 'NONE', #96893 ) ;
#84514=FACE_OUTER_BOUND ( 'NONE', #91592, .T. ) ;
#84516=VECTOR ( 'NONE', #28925, 1000.000000000000000 ) ;
#84518=EDGE_CURVE ( 'NONE', #20632, #58831, #8449, .T. ) ;
#84519=LINE ( 'NONE', #51166, #85624 ) ;
#84521=PLANE ( 'NONE',  #92344 ) ;
#84522=LINE ( 'NONE', #18493, #76757 ) ;
#84523=ORIENTED_EDGE ( 'NONE', *, *, #43411, .F. ) ;
#84524=VECTOR ( 'NONE', #65141, 999.9999999999998863 ) ;
#84525=VERTEX_POINT ( 'NONE', #141139 ) ;
#84526=ORIENTED_EDGE ( 'NONE', *, *, #45467, .T. ) ;
#84527=CARTESIAN_POINT ( 'NONE',  ( 24.79289321881328689, 9.759292476615620160, 5.000000000000000000 ) ) ;
#84528=DIRECTION ( 'NONE',  ( -0.7071067811865486830, -0.7071067811865464625, -0.000000000000000000 ) ) ;
#84529=DIRECTION ( 'NONE',  ( 1.000000000000000000, 0.000000000000000000, 0.000000000000000000 ) ) ;
#84530=DIRECTION ( 'NONE',  ( 0.7071067811865486830, -0.7071067811865464625, -0.000000000000000000 ) ) ;
#84531=PLANE ( 'NONE',  #140838 ) ;
#84533=EDGE_CURVE ( 'NONE', #33763, #11268, #41848, .T. ) ;
#84534=DIRECTION ( 'NONE',  ( 0.000000000000000000, 0.000000000000000000, -1.000000000000000000 ) ) ;
#84535=EDGE_CURVE ( 'NONE', #3663, #85320, #30989, .T. ) ;
#84536=AXIS2_PLACEMENT_3D ( 'NONE', #71698, #16564, #126079 ) ;
#84537=DIRECTION ( 'NONE',  ( 0.7071067811865487940, 0.7071067811865463515, 0.000000000000000000 ) ) ;
#84538=CARTESIAN_POINT ( 'NONE',  ( 1.171830600776456732, 12.75929247661558996, 4.000000000000000000 ) ) ;
#84539=FACE_OUTER_BOUND ( 'NONE', #124944, .T. ) ;
#84541=CARTESIAN_POINT ( 'NONE',  ( -36.18398860626899705, 28.73617430169812437, 5.000000000000000000 ) ) ;
#84542=ORIENTED_EDGE ( 'NONE', *, *, #82166, .F. ) ;
#84543=CARTESIAN_POINT ( 'NONE',  ( -31.41009064519812455, 9.759292476615618384, 11.28811694763771634 ) ) ;
#84544=CARTESIAN_POINT ( 'NONE',  ( -34.75611968250419892, -18.18706574529243625, 4.955485411084906033 ) ) ;
#84545=ORIENTED_EDGE ( 'NONE', *, *, #14102, .T. ) ;
#84546=ADVANCED_FACE ( 'NONE', ( #99048 ), #456, .F. ) ;
#84548=CARTESIAN_POINT ( 'NONE',  ( 8.510786437626906675, -27.52281430457049183, 5.000000000000000000 ) ) ;
#84549=ORIENTED_EDGE ( 'NONE', *, *, #69670, .F. ) ;
#84550=EDGE_LOOP ( 'NONE', ( #60035, #2087, #26264, #63733 ) ) ;
#84551=DIRECTION ( 'NONE',  ( 0.7071067811865487940, 0.7071067811865463515, 0.000000000000000000 ) ) ;
#84552=CARTESIAN_POINT ( 'NONE',  ( -72.48921356237309510, -27.52281430457106026, 5.000000000000000000 ) ) ;
#84553=VECTOR ( 'NONE', #27126, 1000.000000000000000 ) ;
#84555=DIRECTION ( 'NONE',  ( -0.6830127018922180770, -0.6830127018922204085, -0.2588190451025213501 ) ) ;
#84556=VECTOR ( 'NONE', #95162, 1000.000000000000000 ) ;
#84557=VECTOR ( 'NONE', #25076, 1000.000000000000000 ) ;
#84558=FACE_OUTER_BOUND ( 'NONE', #67874, .T. ) ;
#84559=EDGE_LOOP ( 'NONE', ( #104340, #143163, #125458, #27057 ) ) ;
#84563=CARTESIAN_POINT ( 'NONE',  ( -34.92500000000001137, 22.22500000000000142, 4.500000000000000888 ) ) ;
#84564=CARTESIAN_POINT ( 'NONE',  ( -69.48921356237309510, -27.52281430457103895, 5.000000000000000000 ) ) ;
#84565=VERTEX_POINT ( 'NONE', #67169 ) ;
#84566=CARTESIAN_POINT ( 'NONE',  ( -35.99451991528749772, 28.92564299267963079, 4.000000000000000000 ) ) ;
#84567=ORIENTED_EDGE ( 'NONE', *, *, #31913, .F. ) ;
#84569=CARTESIAN_POINT ( 'NONE',  ( 24.18398860626899705, 28.73617430169804265, 5.000000000000000000 ) ) ;
#84571=DIRECTION ( 'NONE',  ( 0.000000000000000000, 0.000000000000000000, -1.000000000000000000 ) ) ;
#84572=ORIENTED_EDGE ( 'NONE', *, *, #81396, .F. ) ;
#84574=FACE_OUTER_BOUND ( 'NONE', #16150, .T. ) ;
#84575=LINE ( 'NONE', #128087, #18467 ) ;
#84576=ADVANCED_FACE ( 'NONE', ( #132465 ), #88941, .F. ) ;
#84577=CARTESIAN_POINT ( 'NONE',  ( -12.18398860626900060, 28.73617430169795739, 5.000000000000000000 ) ) ;
#84578=ORIENTED_EDGE ( 'NONE', *, *, #136069, .T. ) ;
#84580=CARTESIAN_POINT ( 'NONE',  ( -0.7071067811865415775, 17.25929247661554200, 5.000000000000000000 ) ) ;
#84583=VERTEX_POINT ( 'NONE', #131712 ) ;
#84584=ORIENTED_EDGE ( 'NONE', *, *, #74906, .F. ) ;
#84587=ORIENTED_EDGE ( 'NONE', *, *, #42680, .T. ) ;
#84588=ADVANCED_FACE ( 'NONE', ( #65786 ), #111362, .F. ) ;
#84589=CARTESIAN_POINT ( 'NONE',  ( -27.32816939922333432, 14.25929247661558286, 4.000000000000000000 ) ) ;
#84592=CARTESIAN_POINT ( 'NONE',  ( -22.82816939922336630, -17.24070752338410273, 4.000000000000000000 ) ) ;
#84593=ORIENTED_EDGE ( 'NONE', *, *, #7669, .F. ) ;
#84594=EDGE_CURVE ( 'NONE', #138159, #103344, #64314, .T. ) ;
#84595=FACE_OUTER_BOUND ( 'NONE', #92695, .T. ) ;
#84596=CYLINDRICAL_SURFACE ( 'NONE', #337, 0.5000000000000004441 ) ;
#84598=EDGE_CURVE ( 'NONE', #97938, #125706, #45443, .T. ) ;
#84600=LINE ( 'NONE', #83912, #45553 ) ;
#84601=CARTESIAN_POINT ( 'NONE',  ( 36.18398860626899705, 28.73617430169812437, 5.000000000000000000 ) ) ;
#84602=ORIENTED_EDGE ( 'NONE', *, *, #123223, .T. ) ;
#84603=ORIENTED_EDGE ( 'NONE', *, *, #69820, .F. ) ;
#84604=ADVANCED_FACE ( 'NONE', ( #121528 ), #120074, .F. ) ;
#84605=EDGE_CURVE ( 'NONE', #136110, #61441, #1160, .T. ) ;
#84606=LINE ( 'NONE', #60752, #77880 ) ;
#84607=DIRECTION ( 'NONE',  ( 0.6830127018922181881, 0.6830127018922202975, -0.2588190451025214056 ) ) ;
#84608=DIRECTION ( 'NONE',  ( -0.7071067811865486830, -0.7071067811865464625, -0.000000000000000000 ) ) ;
#84609=DIRECTION ( 'NONE',  ( -0.000000000000000000, 0.3543493200069153248, 0.9351131265310292928 ) ) ;
#84610=CARTESIAN_POINT ( 'NONE',  ( 13.49999999999990763, -8.568876922607724822, 4.000000000000000000 ) ) ;
#84611=EDGE_CURVE ( 'NONE', #127621, #77870, #86788, .T. ) ;
#84612=DIRECTION ( 'NONE',  ( 0.6830127018922180770, -0.6830127018922204085, -0.2588190451025213501 ) ) ;
#84614=ORIENTED_EDGE ( 'NONE', *, *, #142037, .T. ) ;
#84615=VERTEX_POINT ( 'NONE', #43993 ) ;
#84616=VERTEX_POINT ( 'NONE', #89623 ) ;
#84617=AXIS2_PLACEMENT_3D ( 'NONE', #54127, #119321, #64256 ) ;
#84618=ORIENTED_EDGE ( 'NONE', *, *, #105814, .F. ) ;
#84619=CARTESIAN_POINT ( 'NONE',  ( -34.92500000000001137, 3.856123077392404674, 4.000000000000000000 ) ) ;
#84620=ORIENTED_EDGE ( 'NONE', *, *, #94563, .T. ) ;
#84621=CARTESIAN_POINT ( 'NONE',  ( -27.48921356237309155, -27.52281430457074762, 5.000000000000000000 ) ) ;
#84622=CARTESIAN_POINT ( 'NONE',  ( 5.292893218813425449, 5.259292476615663681, 5.000000000000000000 ) ) ;
#84623=EDGE_CURVE ( 'NONE', #136452, #140795, #66468, .T. ) ;
#84624=CARTESIAN_POINT ( 'NONE',  ( 6.005480084712508493, 28.92564299267933947, 4.000000000000000000 ) ) ;
#84625=CARTESIAN_POINT ( 'NONE',  ( -32.99999999999976552, -12.41253812416063163, 4.000000000000000000 ) ) ;
#84626=VERTEX_POINT ( 'NONE', #142594 ) ;
#84627=CARTESIAN_POINT ( 'NONE',  ( 33.79333936457825160, 21.75929247661550647, 4.998822639870711626 ) ) ;
#84631=ORIENTED_EDGE ( 'NONE', *, *, #83930, .F. ) ;
#84633=ORIENTED_EDGE ( 'NONE', *, *, #104414, .F. ) ;
#84635=ORIENTED_EDGE ( 'NONE', *, *, #11933, .F. ) ;
#84636=ORIENTED_EDGE ( 'NONE', *, *, #90760, .F. ) ;
#84637=VECTOR ( 'NONE', #85423, 1000.000000000000000 ) ;
#84638=DIRECTION ( 'NONE',  ( -0.7071067811865487940, 0.7071067811865463515, 0.000000000000000000 ) ) ;
#84639=VECTOR ( 'NONE', #128949, 1000.000000000000000 ) ;
#84640=DIRECTION ( 'NONE',  ( 1.000000000000000000, -0.000000000000000000, 0.000000000000000000 ) ) ;
#84642=LINE ( 'NONE', #127416, #40218 ) ;
#84643=VECTOR ( 'NONE', #80587, 1000.000000000000000 ) ;
#84644=EDGE_CURVE ( 'NONE', #108030, #26817, #75212, .T. ) ;
#84645=CARTESIAN_POINT ( 'NONE',  ( 0.000000000000000000, 0.000000000000000000, 5.000000000000000000 ) ) ;
#84646=FACE_OUTER_BOUND ( 'NONE', #73924, .T. ) ;
#84647=DIRECTION ( 'NONE',  ( 0.000000000000000000, 0.3543493200069153248, 0.9351131265310291818 ) ) ;
#84649=CARTESIAN_POINT ( 'NONE',  ( -9.183988606268997046, 28.73617430169793607, 5.000000000000000000 ) ) ;
#84652=ORIENTED_EDGE ( 'NONE', *, *, #132423, .F. ) ;
#84653=CARTESIAN_POINT ( 'NONE',  ( 26.99451991528749417, 28.92564299267956685, 4.000000000000000000 ) ) ;
#84654=FACE_OUTER_BOUND ( 'NONE', #101661, .T. ) ;
#84655=ADVANCED_FACE ( 'NONE', ( #99780 ), #31684, .F. ) ;
#84656=VERTEX_POINT ( 'NONE', #78764 ) ;
#84657=ORIENTED_EDGE ( 'NONE', *, *, #4876, .F. ) ;
#84658=ORIENTED_EDGE ( 'NONE', *, *, #73571, .F. ) ;
#84659=ORIENTED_EDGE ( 'NONE', *, *, #42233, .T. ) ;
#84660=DIRECTION ( 'NONE',  ( 0.7071067811865487940, 0.7071067811865463515, -0.000000000000000000 ) ) ;
#84661=CARTESIAN_POINT ( 'NONE',  ( -51.48921356237309510, -27.52281430457091460, 5.000000000000000000 ) ) ;
#84663=CARTESIAN_POINT ( 'NONE',  ( -5.999999999999960032, 1.931123077392169041, 4.000000000000000000 ) ) ;
#84665=VERTEX_POINT ( 'NONE', #122975 ) ;
#84667=ORIENTED_EDGE ( 'NONE', *, *, #100962, .F. ) ;
#84669=DIRECTION ( 'NONE',  ( 0.7071067811865487940, 0.7071067811865463515, -0.000000000000000000 ) ) ;
#84670=LINE ( 'NONE', #96221, #113054 ) ;
#84671=LINE ( 'NONE', #108516, #83694 ) ;
#84672=ORIENTED_EDGE ( 'NONE', *, *, #83000, .T. ) ;
#84674=ORIENTED_EDGE ( 'NONE', *, *, #56255, .F. ) ;
#84675=DIRECTION ( 'NONE',  ( 0.7071067811865486830, -0.7071067811865464625, -0.000000000000000000 ) ) ;
#84676=DIRECTION ( 'NONE',  ( 0.7071067811865487940, 0.7071067811865463515, -0.000000000000000000 ) ) ;
#84680=CARTESIAN_POINT ( 'NONE',  ( 3.299744871391591339, -27.71228299555208352, 4.000000000000000000 ) ) ;
#84681=CARTESIAN_POINT ( 'NONE',  ( -23.99999999999983302, -12.41253812416062274, 4.000000000000000000 ) ) ;
#84683=EDGE_CURVE ( 'NONE', #134910, #124430, #141557, .T. ) ;
#84685=DIRECTION ( 'NONE',  ( 0.7071067811865487940, 0.7071067811865463515, -0.000000000000000000 ) ) ;
#84687=ORIENTED_EDGE ( 'NONE', *, *, #120584, .F. ) ;
#84688=CARTESIAN_POINT ( 'NONE',  ( -14.99451991528749595, 28.92564299267948513, 4.000000000000000000 ) ) ;
#84690=ORIENTED_EDGE ( 'NONE', *, *, #22672, .T. ) ;
#84692=DIRECTION ( 'NONE',  ( 1.000000000000000000, 0.000000000000000000, 0.000000000000000000 ) ) ;
#84693=ORIENTED_EDGE ( 'NONE', *, *, #28073, .T. ) ;
#84694=EDGE_CURVE ( 'NONE', #60397, #59481, #82877, .T. ) ;
#84695=CARTESIAN_POINT ( 'NONE',  ( 29.29289321881324781, 14.25929247661557042, 5.000000000000000000 ) ) ;
#84696=CARTESIAN_POINT ( 'NONE',  ( 26.29289321881327268, -9.740707523384187994, 5.000000000000000000 ) ) ;
#84697=ORIENTED_EDGE ( 'NONE', *, *, #34285, .T. ) ;
#84698=DIRECTION ( 'NONE',  ( 1.000000000000000000, 0.000000000000000000, 0.000000000000000000 ) ) ;
#84699=ORIENTED_EDGE ( 'NONE', *, *, #43251, .T. ) ;
#84702=AXIS2_PLACEMENT_3D ( 'NONE', #137471, #47638, #25836 ) ;
#84704=LINE ( 'NONE', #110010, #62385 ) ;
#84705=LINE ( 'NONE', #49252, #39002 ) ;
#84706=VECTOR ( 'NONE', #110409, 1000.000000000000000 ) ;
#84707=FACE_OUTER_BOUND ( 'NONE', #16350, .T. ) ;
#84712=CARTESIAN_POINT ( 'NONE',  ( 12.18398860626900060, 28.73617430169795739, 5.000000000000000000 ) ) ;
#84713=ORIENTED_EDGE ( 'NONE', *, *, #3995, .T. ) ;
#84714=ADVANCED_FACE ( 'NONE', ( #49551 ), #106003, .F. ) ;
#84716=ORIENTED_EDGE ( 'NONE', *, *, #99233, .F. ) ;
#84718=LINE ( 'NONE', #62267, #67551 ) ;
#84719=ORIENTED_EDGE ( 'NONE', *, *, #7716, .F. ) ;
#84720=VECTOR ( 'NONE', #29955, 1000.000000000000000 ) ;
#84721=FACE_OUTER_BOUND ( 'NONE', #23929, .T. ) ;
#84722=FACE_OUTER_BOUND ( 'NONE', #130741, .T. ) ;
#84723=CARTESIAN_POINT ( 'NONE',  ( 13.49999999999991118, 19.08746187583904685, 4.000000000000000000 ) ) ;
#84724=ORIENTED_EDGE ( 'NONE', *, *, #73374, .F. ) ;
#84725=DIRECTION ( 'NONE',  ( -0.7071067811865486830, -0.7071067811865464625, 0.000000000000000000 ) ) ;
#84726=CARTESIAN_POINT ( 'NONE',  ( -8.540161610502543965, 18.75929247661552424, 8.305906642995466882 ) ) ;
#84728=LINE ( 'NONE', #120170, #79645 ) ;
#84729=LINE ( 'NONE', #95596, #105291 ) ;
#84730=VERTEX_POINT ( 'NONE', #23657 ) ;
#84731=DIRECTION ( 'NONE',  ( 1.000000000000000000, 0.000000000000000000, 0.000000000000000000 ) ) ;
#84732=DIRECTION ( 'NONE',  ( -0.7071067811865486830, -0.7071067811865464625, -0.000000000000000000 ) ) ;
#84733=FACE_OUTER_BOUND ( 'NONE', #20745, .T. ) ;
#84734=CARTESIAN_POINT ( 'NONE',  ( 27.47336096364197644, -5.240707523384228850, 16.25846745537502258 ) ) ;
#84735=LINE ( 'NONE', #77978, #84639 ) ;
#84736=VECTOR ( 'NONE', #68714, 1000.000000000000000 ) ;
#84738=ORIENTED_EDGE ( 'NONE', *, *, #13932, .T. ) ;
#84739=VERTEX_POINT ( 'NONE', #34539 ) ;
#84741=ADVANCED_FACE ( 'NONE', ( #79523 ), #6673, .F. ) ;
#84744=EDGE_CURVE ( 'NONE', #72622, #65156, #95150, .T. ) ;
#84745=VECTOR ( 'NONE', #78326, 999.9999999999998863 ) ;
#84749=ORIENTED_EDGE ( 'NONE', *, *, #46183, .F. ) ;
#84750=EDGE_CURVE ( 'NONE', #93317, #121222, #50955, .T. ) ;
#84751=ADVANCED_FACE ( 'NONE', ( #4511 ), #60426, .T. ) ;
#84752=DIRECTION ( 'NONE',  ( -0.7071067811865486830, -0.7071067811865464625, 0.000000000000000000 ) ) ;
#84753=CARTESIAN_POINT ( 'NONE',  ( -25.49999999999982236, 8.319652575858368593, -8.582050562765886070 ) ) ;
#84755=ORIENTED_EDGE ( 'NONE', *, *, #36486, .F. ) ;
#84756=LINE ( 'NONE', #83337, #102244 ) ;
#84757=VERTEX_POINT ( 'NONE', #67924 ) ;
#84760=LINE ( 'NONE', #107214, #124956 ) ;
#84761=ORIENTED_EDGE ( 'NONE', *, *, #53086, .T. ) ;
#84762=ORIENTED_EDGE ( 'NONE', *, *, #20971, .T. ) ;
#84763=ADVANCED_FACE ( 'NONE', ( #37947 ), #57034, .F. ) ;
#84764=ORIENTED_EDGE ( 'NONE', *, *, #57935, .F. ) ;
#84765=DIRECTION ( 'NONE',  ( 0.7071067811865487940, 0.7071067811865463515, 0.000000000000000000 ) ) ;
#84767=PLANE ( 'NONE',  #8293 ) ;
#84769=DIRECTION ( 'NONE',  ( -0.7071067811865486830, -0.7071067811865464625, -0.000000000000000000 ) ) ;
#84770=EDGE_CURVE ( 'NONE', #35713, #112904, #59701, .T. ) ;
#84772=EDGE_LOOP ( 'NONE', ( #111393, #76803, #65106, #76483 ) ) ;
#84773=ORIENTED_EDGE ( 'NONE', *, *, #128575, .T. ) ;
#84774=FACE_OUTER_BOUND ( 'NONE', #73230, .T. ) ;
#84775=ORIENTED_EDGE ( 'NONE', *, *, #27406, .T. ) ;
#84777=EDGE_CURVE ( 'NONE', #58187, #19888, #105313, .T. ) ;
#84778=VECTOR ( 'NONE', #51226, 1000.000000000000000 ) ;
#84780=CARTESIAN_POINT ( 'NONE',  ( 12.32816939922344623, 11.25929247661559884, 4.000000000000000000 ) ) ;
#84782=LINE ( 'NONE', #106492, #89971 ) ;
#84783=CARTESIAN_POINT ( 'NONE',  ( 9.792893218813388145, 6.759292476615649470, 5.000000000000000000 ) ) ;
#84784=ADVANCED_FACE ( 'NONE', ( #115440 ), #134585, .F. ) ;
#84786=DIRECTION ( 'NONE',  ( -0.000000000000000000, -0.3543493200069152693, 0.9351131265310292928 ) ) ;
#84788=ORIENTED_EDGE ( 'NONE', *, *, #142397, .F. ) ;
#84789=CARTESIAN_POINT ( 'NONE',  ( -30.29974487139158867, -27.71228299555227537, 4.000000000000000000 ) ) ;
#84790=CARTESIAN_POINT ( 'NONE',  ( -47.99451991528749062, 28.92564299267971251, 4.000000000000000000 ) ) ;
#84792=CARTESIAN_POINT ( 'NONE',  ( -32.16347128873431416, 15.75929247661555443, 9.299976744542847840 ) ) ;
#84793=LINE ( 'NONE', #39155, #24902 ) ;
#84795=ORIENTED_EDGE ( 'NONE', *, *, #71161, .F. ) ;
#84796=DIRECTION ( 'NONE',  ( -0.6830127018922180770, -0.6830127018922204085, -0.2588190451025213501 ) ) ;
#84797=ORIENTED_EDGE ( 'NONE', *, *, #71672, .T. ) ;
#84798=ORIENTED_EDGE ( 'NONE', *, *, #108085, .F. ) ;
#84799=ORIENTED_EDGE ( 'NONE', *, *, #28506, .F. ) ;
#84800=EDGE_CURVE ( 'NONE', #41198, #101203, #61165, .T. ) ;
#84801=VECTOR ( 'NONE', #3127, 999.9999999999998863 ) ;
#84802=CARTESIAN_POINT ( 'NONE',  ( 34.42499999999998295, -21.72500000000000142, 5.000000000000000000 ) ) ;
#84803=CARTESIAN_POINT ( 'NONE',  ( -20.84387692260743918, -22.22500000000000142, 4.000000000000000000 ) ) ;
#84804=CARTESIAN_POINT ( 'NONE',  ( 3.299744871391591339, -27.71228299555208352, 4.000000000000000000 ) ) ;
#84805=VECTOR ( 'NONE', #102067, 999.9999999999998863 ) ;
#84806=DIRECTION ( 'NONE',  ( -0.000000000000000000, 0.000000000000000000, 1.000000000000000000 ) ) ;
#84807=CARTESIAN_POINT ( 'NONE',  ( 0.000000000000000000, 0.000000000000000000, 5.000000000000000000 ) ) ;
#84808=PLANE ( 'NONE',  #34377 ) ;
#84809=PLANE ( 'NONE',  #29583 ) ;
#84810=CARTESIAN_POINT ( 'NONE',  ( -24.75860074219779605, 21.72500000000000853, 5.000000000000000000 ) ) ;
#84811=CARTESIAN_POINT ( 'NONE',  ( -12.48921356237309155, -27.52281430457064104, 5.000000000000000000 ) ) ;
#84812=CARTESIAN_POINT ( 'NONE',  ( 38.99451991528749062, 28.92564299267965211, 4.000000000000000000 ) ) ;
#84813=CARTESIAN_POINT ( 'NONE',  ( 33.29974487139158867, -27.71228299555229313, 4.000000000000000000 ) ) ;
#84815=VECTOR ( 'NONE', #11289, 1000.000000000000000 ) ;
#84816=EDGE_CURVE ( 'NONE', #49512, #79543, #83597, .T. ) ;
#84817=ORIENTED_EDGE ( 'NONE', *, *, #129572, .F. ) ;
#84818=ORIENTED_EDGE ( 'NONE', *, *, #122931, .T. ) ;
#84820=ORIENTED_EDGE ( 'NONE', *, *, #10092, .F. ) ;
#84821=DIRECTION ( 'NONE',  ( 0.6830127018922181881, 0.6830127018922202975, -0.2588190451025214056 ) ) ;
#84822=ORIENTED_EDGE ( 'NONE', *, *, #49900, .F. ) ;
#84823=ORIENTED_EDGE ( 'NONE', *, *, #35640, .F. ) ;
#84824=DIRECTION ( 'NONE',  ( -0.7071067811865487940, 0.7071067811865463515, 0.000000000000000000 ) ) ;
#84825=FACE_OUTER_BOUND ( 'NONE', #21903, .T. ) ;
#84827=ADVANCED_FACE ( 'NONE', ( #95866 ), #42231, .F. ) ;
#84828=DIRECTION ( 'NONE',  ( 0.7071067811865487940, 0.7071067811865463515, 0.000000000000000000 ) ) ;
#84829=ORIENTED_EDGE ( 'NONE', *, *, #6836, .T. ) ;
#84830=DIRECTION ( 'NONE',  ( -0.3543493200069162685, -0.000000000000000000, -0.9351131265310288487 ) ) ;
#84831=VERTEX_POINT ( 'NONE', #120434 ) ;
#84832=AXIS2_PLACEMENT_3D ( 'NONE', #117013, #20538, #8222 ) ;
#84834=DIRECTION ( 'NONE',  ( -0.7071067811865486830, 0.7071067811865464625, 0.000000000000000000 ) ) ;
#84835=LINE ( 'NONE', #52886, #38085 ) ;
#84836=VECTOR ( 'NONE', #79568, 1000.000000000000227 ) ;
#84838=ORIENTED_EDGE ( 'NONE', *, *, #117272, .F. ) ;
#84841=ORIENTED_EDGE ( 'NONE', *, *, #50801, .T. ) ;
#84842=ORIENTED_EDGE ( 'NONE', *, *, #34294, .F. ) ;
#84843=CARTESIAN_POINT ( 'NONE',  ( -20.20710678118640757, 15.75929247661555976, 5.000000000000000000 ) ) ;
#84844=EDGE_LOOP ( 'NONE', ( #90944, #74680, #121498 ) ) ;
#84845=DIRECTION ( 'NONE',  ( 0.7071067811865487940, 0.7071067811865463515, -0.000000000000000000 ) ) ;
#84847=VECTOR ( 'NONE', #6378, 999.9999999999998863 ) ;
#84848=DIRECTION ( 'NONE',  ( -0.7071067811865487940, 0.7071067811865463515, 0.000000000000000000 ) ) ;
#84849=DIRECTION ( 'NONE',  ( 0.7071067811865486830, -0.7071067811865464625, -0.000000000000000000 ) ) ;
#84850=ORIENTED_EDGE ( 'NONE', *, *, #85678, .T. ) ;
#84851=CARTESIAN_POINT ( 'NONE',  ( 77.99451991528749772, 28.92564299267992567, 4.000000000000000000 ) ) ;
#84852=EDGE_CURVE ( 'NONE', #73074, #108741, #25022, .T. ) ;
#84853=PLANE ( 'NONE',  #39708 ) ;
#84856=PLANE ( 'NONE',  #28169 ) ;
#84857=DIRECTION ( 'NONE',  ( 0.7071067811865486830, -0.7071067811865464625, -0.000000000000000000 ) ) ;
#84858=ORIENTED_EDGE ( 'NONE', *, *, #50535, .F. ) ;
#84859=EDGE_CURVE ( 'NONE', #143176, #48427, #64680, .T. ) ;
#84860=DIRECTION ( 'NONE',  ( -0.7071067811865486830, 0.7071067811865464625, 0.000000000000000000 ) ) ;
#84861=ORIENTED_EDGE ( 'NONE', *, *, #133193, .T. ) ;
#84862=VERTEX_POINT ( 'NONE', #74128 ) ;
#84863=EDGE_CURVE ( 'NONE', #55719, #7189, #98022, .T. ) ;
#84864=LINE ( 'NONE', #11549, #104918 ) ;
#84865=CARTESIAN_POINT ( 'NONE',  ( -5.999999999999960032, -3.485240976185084882, -4.108735105802409748 ) ) ;
#84866=ORIENTED_EDGE ( 'NONE', *, *, #51620, .T. ) ;
#84867=DIRECTION ( 'NONE',  ( 0.7071067811865487940, -0.7071067811865463515, 0.000000000000000000 ) ) ;
#84868=CARTESIAN_POINT ( 'NONE',  ( -24.21271579574130683, 0.1791150535437372460, 5.000000000000000000 ) ) ;
#84869=AXIS2_PLACEMENT_3D ( 'NONE', #15093, #103524, #60808 ) ;
#84870=PLANE ( 'NONE',  #55355 ) ;
#84871=EDGE_CURVE ( 'NONE', #104733, #60519, #65742, .T. ) ;
#84872=CARTESIAN_POINT ( 'NONE',  ( 0.000000000000000000, 0.000000000000000000, 5.000000000000000000 ) ) ;
#84873=CARTESIAN_POINT ( 'NONE',  ( 23.99999999999984013, 11.96639925780213964, 5.000000000000000000 ) ) ;
#84874=CARTESIAN_POINT ( 'NONE',  ( -22.49999999999984723, -11.56887692260769640, 4.000000000000000000 ) ) ;
#84876=PLANE ( 'NONE',  #132257 ) ;
#84877=FACE_OUTER_BOUND ( 'NONE', #85711, .T. ) ;
#84879=VECTOR ( 'NONE', #137890, 999.9999999999998863 ) ;
#84882=DIRECTION ( 'NONE',  ( -0.000000000000000000, -0.3543493200069152693, 0.9351131265310292928 ) ) ;
#84883=ORIENTED_EDGE ( 'NONE', *, *, #22758, .T. ) ;
#84886=EDGE_LOOP ( 'NONE', ( #62024, #83049, #122148, #76543 ) ) ;
#84888=ORIENTED_EDGE ( 'NONE', *, *, #82969, .T. ) ;
#84889=ORIENTED_EDGE ( 'NONE', *, *, #135286, .T. ) ;
#84892=VERTEX_POINT ( 'NONE', #31341 ) ;
#84894=LINE ( 'NONE', #96445, #134355 ) ;
#84895=LINE ( 'NONE', #106616, #111184 ) ;
#84896=AXIS2_PLACEMENT_3D ( 'NONE', #32737, #9501, #122560 ) ;
#84897=CARTESIAN_POINT ( 'NONE',  ( -0.7928932188134485415, 15.75929247661555443, 5.000000000000000000 ) ) ;
#84899=ORIENTED_EDGE ( 'NONE', *, *, #10991, .T. ) ;
#84900=CARTESIAN_POINT ( 'NONE',  ( 34.92499999999998295, 22.22500000000000142, 4.500000000000000888 ) ) ;
#84902=CARTESIAN_POINT ( 'NONE',  ( -2.999999999999973355, 2.587461875839211167, 4.000000000000000000 ) ) ;
#84904=DIRECTION ( 'NONE',  ( 0.6830127018922181881, 0.6830127018922202975, -0.2588190451025214056 ) ) ;
#84906=PLANE ( 'NONE',  #12702 ) ;
#84908=PLANE ( 'NONE',  #30530 ) ;
#84909=LINE ( 'NONE', #7324, #69447 ) ;
#84910=ORIENTED_EDGE ( 'NONE', *, *, #60055, .F. ) ;
#84912=ADVANCED_FACE ( 'NONE', ( #19728 ), #108856, .T. ) ;
#84915=ORIENTED_EDGE ( 'NONE', *, *, #51267, .T. ) ;
#84917=EDGE_CURVE ( 'NONE', #110456, #135979, #53063, .T. ) ;
#84918=CARTESIAN_POINT ( 'NONE',  ( -30.70710678118632231, -0.7407075233842788098, 5.000000000000000000 ) ) ;
#84920=CARTESIAN_POINT ( 'NONE',  ( 15.18398860626900237, 28.73617430169797871, 5.000000000000000000 ) ) ;
#84921=EDGE_CURVE ( 'NONE', #113570, #48874, #84995, .T. ) ;
#84922=EDGE_CURVE ( 'NONE', #35574, #16896, #10273, .T. ) ;
#84923=CARTESIAN_POINT ( 'NONE',  ( -34.92500000000001137, -22.22500000000000142, 4.000000000000000000 ) ) ;
#84924=CARTESIAN_POINT ( 'NONE',  ( -39.18398860626899705, 28.73617430169814568, 5.000000000000000000 ) ) ;
#84927=LINE ( 'NONE', #129139, #135868 ) ;
#84928=ORIENTED_EDGE ( 'NONE', *, *, #43361, .F. ) ;
#84930=DIRECTION ( 'NONE',  ( -0.7071067811865486830, 0.7071067811865464625, 0.000000000000000000 ) ) ;
#84931=CARTESIAN_POINT ( 'NONE',  ( 32.71998032010576196, 0.7592924766157138627, 14.27032725228016474 ) ) ;
#84932=CARTESIAN_POINT ( 'NONE',  ( 29.20666063542132207, 21.75929247661549581, 4.998822639870703632 ) ) ;
#84933=VERTEX_POINT ( 'NONE', #107452 ) ;
#84935=EDGE_CURVE ( 'NONE', #127280, #52226, #9547, .T. ) ;
#84936=ORIENTED_EDGE ( 'NONE', *, *, #3516, .F. ) ;
#84937=DIRECTION ( 'NONE',  ( -0.7071067811865486830, -0.7071067811865464625, -0.000000000000000000 ) ) ;
#84938=ADVANCED_FACE ( 'NONE', ( #52362 ), #40106, .F. ) ;
#84939=CARTESIAN_POINT ( 'NONE',  ( 36.48921356237310221, -27.52281430457080802, 5.000000000000000000 ) ) ;
#84940=LINE ( 'NONE', #73372, #138134 ) ;
#84941=FACE_OUTER_BOUND ( 'NONE', #96091, .T. ) ;
#84942=AXIS2_PLACEMENT_3D ( 'NONE', #118258, #105950, #141468 ) ;
#84944=VECTOR ( 'NONE', #11059, 1000.000000000000000 ) ;
#84945=EDGE_CURVE ( 'NONE', #76170, #98656, #119044, .T. ) ;
#84947=VERTEX_POINT ( 'NONE', #119732 ) ;
#84948=AXIS2_PLACEMENT_3D ( 'NONE', #28929, #82598, #92740 ) ;
#84949=LINE ( 'NONE', #118265, #22397 ) ;
#84950=ORIENTED_EDGE ( 'NONE', *, *, #3880, .F. ) ;
#84951=EDGE_LOOP ( 'NONE', ( #19106, #111812, #107784, #35262 ) ) ;
#84955=DIRECTION ( 'NONE',  ( 0.7071067811865487940, -0.7071067811865463515, 0.000000000000000000 ) ) ;
#84956=ORIENTED_EDGE ( 'NONE', *, *, #94309, .T. ) ;
#84957=ADVANCED_FACE ( 'NONE', ( #117588 ), #76277, .F. ) ;
#84958=LINE ( 'NONE', #129164, #94528 ) ;
#84960=FACE_BOUND ( 'NONE', #110240, .T. ) ;
#84962=FACE_OUTER_BOUND ( 'NONE', #119960, .T. ) ;
#84963=DIRECTION ( 'NONE',  ( 0.7071067811865486830, -0.7071067811865464625, -0.000000000000000000 ) ) ;
#84964=FACE_OUTER_BOUND ( 'NONE', #11629, .T. ) ;
#84965=ORIENTED_EDGE ( 'NONE', *, *, #51208, .T. ) ;
#84967=VERTEX_POINT ( 'NONE', #1518 ) ;
#84968=VECTOR ( 'NONE', #91763, 1000.000000000000000 ) ;
#84969=EDGE_CURVE ( 'NONE', #101903, #142842, #77705, .T. ) ;
#84970=ORIENTED_EDGE ( 'NONE', *, *, #23717, .T. ) ;
#84971=LINE ( 'NONE', #95120, #74910 ) ;
#84972=ORIENTED_EDGE ( 'NONE', *, *, #70273, .T. ) ;
#84975=VECTOR ( 'NONE', #394, 999.9999999999998863 ) ;
#84976=EDGE_LOOP ( 'NONE', ( #24216, #131151, #81419, #36731 ) ) ;
#84977=CARTESIAN_POINT ( 'NONE',  ( -19.49999999999986500, 21.05218569542895679, 5.000000000000000000 ) ) ;
#84978=DIRECTION ( 'NONE',  ( -0.6830127018922180770, -0.6830127018922204085, -0.2588190451025213501 ) ) ;
#84979=ORIENTED_EDGE ( 'NONE', *, *, #27720, .T. ) ;
#84980=CARTESIAN_POINT ( 'NONE',  ( 25.49999999999981526, 7.087461875839178305, 4.000000000000000000 ) ) ;
#84982=ADVANCED_FACE ( 'NONE', ( #11679 ), #112463, .F. ) ;
#84983=PLANE ( 'NONE',  #73342 ) ;
#84984=DIRECTION ( 'NONE',  ( -0.000000000000000000, -0.3543493200069152693, 0.9351131265310292928 ) ) ;
#84985=CARTESIAN_POINT ( 'NONE',  ( 33.72281430457037743, -21.72499999999999432, 5.000000000000000000 ) ) ;
#84986=CARTESIAN_POINT ( 'NONE',  ( -24.29974487139158867, -27.71228299555223273, 4.000000000000000000 ) ) ;
#84987=ORIENTED_EDGE ( 'NONE', *, *, #9853, .T. ) ;
#84988=VECTOR ( 'NONE', #111649, 1000.000000000000000 ) ;
#84989=ORIENTED_EDGE ( 'NONE', *, *, #111411, .T. ) ;
#84990=CARTESIAN_POINT ( 'NONE',  ( -23.99451991528749062, 28.92564299267954908, 4.000000000000000000 ) ) ;
#84991=DIRECTION ( 'NONE',  ( 0.6830127018922181881, 0.6830127018922202975, -0.2588190451025214056 ) ) ;
#84992=ORIENTED_EDGE ( 'NONE', *, *, #57272, .F. ) ;
#84993=VERTEX_POINT ( 'NONE', #45108 ) ;
#84994=VERTEX_POINT ( 'NONE', #133508 ) ;
#84995=LINE ( 'NONE', #7413, #32811 ) ;
#84996=CARTESIAN_POINT ( 'NONE',  ( 26.99999999999981171, -12.41253812416062985, 4.000000000000000000 ) ) ;
#84997=ORIENTED_EDGE ( 'NONE', *, *, #18424, .F. ) ;
#85001=LINE ( 'NONE', #63298, #79666 ) ;
#85002=VERTEX_POINT ( 'NONE', #2228 ) ;
#85004=VECTOR ( 'NONE', #61809, 1000.000000000000000 ) ;
#85007=CARTESIAN_POINT ( 'NONE',  ( -33.29974487139158867, -27.71228299555229313, 4.000000000000000000 ) ) ;
#85008=DIRECTION ( 'NONE',  ( -0.000000000000000000, 0.3543493200069153248, 0.9351131265310292928 ) ) ;
#85009=EDGE_LOOP ( 'NONE', ( #137492, #25948, #36377, #7829 ) ) ;
#85010=DIRECTION ( 'NONE',  ( -0.000000000000000000, 0.000000000000000000, 1.000000000000000000 ) ) ;
#85013=DIRECTION ( 'NONE',  ( 0.7071067811865486830, -0.7071067811865464625, -0.000000000000000000 ) ) ;
#85015=ORIENTED_EDGE ( 'NONE', *, *, #14695, .F. ) ;
#85016=PLANE ( 'NONE',  #19462 ) ;
#85017=FACE_OUTER_BOUND ( 'NONE', #65526, .T. ) ;
#85019=ORIENTED_EDGE ( 'NONE', *, *, #76377, .T. ) ;
#85020=CARTESIAN_POINT ( 'NONE',  ( 48.29974487139158867, -27.71228299555239971, 4.000000000000000000 ) ) ;
#85021=CARTESIAN_POINT ( 'NONE',  ( -11.99999999999991296, -7.447814304570750998, 5.000000000000000000 ) ) ;
#85023=PLANE ( 'NONE',  #116600 ) ;
#85024=VECTOR ( 'NONE', #118814, 1000.000000000000000 ) ;
#85025=DIRECTION ( 'NONE',  ( 0.7071067811865486830, -0.7071067811865464625, -0.000000000000000000 ) ) ;
#85026=EDGE_CURVE ( 'NONE', #118046, #135054, #134960, .T. ) ;
#85028=EDGE_CURVE ( 'NONE', #90677, #23319, #124053, .T. ) ;
#85029=ORIENTED_EDGE ( 'NONE', *, *, #103889, .T. ) ;
#85030=DIRECTION ( 'NONE',  ( 0.7071067811865486830, -0.7071067811865464625, -0.000000000000000000 ) ) ;
#85031=DIRECTION ( 'NONE',  ( -0.7071067811865486830, -0.7071067811865464625, 0.000000000000000000 ) ) ;
#85032=VECTOR ( 'NONE', #12720, 1000.000000000000000 ) ;
#85033=VECTOR ( 'NONE', #73205, 999.9999999999998863 ) ;
#85034=EDGE_CURVE ( 'NONE', #49673, #9354, #12419, .T. ) ;
#85036=LINE ( 'NONE', #16178, #75956 ) ;
#85038=CARTESIAN_POINT ( 'NONE',  ( 14.99999999999989519, 7.559798855135672291, 4.979909187984731922 ) ) ;
#85040=EDGE_LOOP ( 'NONE', ( #108961, #57259, #53216, #85382 ) ) ;
#85043=FACE_OUTER_BOUND ( 'NONE', #131212, .T. ) ;
#85044=LINE ( 'NONE', #53873, #109544 ) ;
#85045=VECTOR ( 'NONE', #78896, 999.9999999999998863 ) ;
#85046=PLANE ( 'NONE',  #25153 ) ;
#85048=CARTESIAN_POINT ( 'NONE',  ( 12.18398860626900060, 28.73617430169795739, 5.000000000000000000 ) ) ;
#85049=ADVANCED_FACE ( 'NONE', ( #91432 ), #25429, .F. ) ;
#85050=ORIENTED_EDGE ( 'NONE', *, *, #29537, .F. ) ;
#85051=CARTESIAN_POINT ( 'NONE',  ( 0.000000000000000000, 0.000000000000000000, 5.000000000000000000 ) ) ;
#85053=EDGE_LOOP ( 'NONE', ( #132481, #139197, #131941, #88958 ) ) ;
#85054=LINE ( 'NONE', #28556, #112626 ) ;
#85055=CARTESIAN_POINT ( 'NONE',  ( -29.99999999999979039, 4.384688058510544550, -7.090945410444755126 ) ) ;
#85056=ADVANCED_FACE ( 'NONE', ( #104420 ), #126194, .F. ) ;
#85057=PLANE ( 'NONE',  #124793 ) ;
#85058=CARTESIAN_POINT ( 'NONE',  ( -5.816011393731002066, 28.73617430169783304, 5.000000000000000000 ) ) ;
#85059=DIRECTION ( 'NONE',  ( 0.7071067811865487940, 0.7071067811865463515, -0.000000000000000000 ) ) ;
#85060=CARTESIAN_POINT ( 'NONE',  ( 0.000000000000000000, 0.000000000000000000, 5.000000000000000000 ) ) ;
#85062=ORIENTED_EDGE ( 'NONE', *, *, #25728, .T. ) ;
#85063=CARTESIAN_POINT ( 'NONE',  ( 34.92499999999998295, 8.816654386410357702, 4.500000000000000888 ) ) ;
#85064=DIRECTION ( 'NONE',  ( 0.7071067811865486830, -0.7071067811865464625, -0.000000000000000000 ) ) ;
#85066=EDGE_CURVE ( 'NONE', #88846, #82235, #5083, .T. ) ;
#85067=CARTESIAN_POINT ( 'NONE',  ( -34.92500000000001137, -22.22500000000000142, 4.000000000000000000 ) ) ;
#85068=ADVANCED_FACE ( 'NONE', ( #127626 ), #26171, .F. ) ;
#85069=FACE_OUTER_BOUND ( 'NONE', #88954, .T. ) ;
#85071=PLANE ( 'NONE',  #8696 ) ;
#85073=VECTOR ( 'NONE', #9201, 1000.000000000000000 ) ;
#85074=CARTESIAN_POINT ( 'NONE',  ( -2.700255128608413990, -27.71228299555204089, 4.000000000000000000 ) ) ;
#85076=EDGE_LOOP ( 'NONE', ( #106926, #19572, #12800, #50128 ) ) ;
#85078=CARTESIAN_POINT ( 'NONE',  ( -32.14114312045509081, 22.22500000000000142, 6.054907437694478034 ) ) ;
#85079=CARTESIAN_POINT ( 'NONE',  ( 11.99451991528749417, 28.92564299267946382, 4.000000000000000000 ) ) ;
#85081=VECTOR ( 'NONE', #63576, 1000.000000000000000 ) ;
#85082=DIRECTION ( 'NONE',  ( -0.7071067811865487940, 0.7071067811865463515, -0.000000000000000000 ) ) ;
#85084=LINE ( 'NONE', #129289, #25929 ) ;
#85085=EDGE_CURVE ( 'NONE', #21635, #86313, #70437, .T. ) ;
#85088=ORIENTED_EDGE ( 'NONE', *, *, #475, .T. ) ;
#85089=DIRECTION ( 'NONE',  ( -0.7071067811865486830, -0.7071067811865464625, 0.000000000000000000 ) ) ;
#85090=ORIENTED_EDGE ( 'NONE', *, *, #103393, .F. ) ;
#85091=ORIENTED_EDGE ( 'NONE', *, *, #58353, .T. ) ;
#85092=PLANE ( 'NONE',  #116401 ) ;
#85093=ADVANCED_FACE ( 'NONE', ( #114581 ), #93566, .F. ) ;
#85094=DIRECTION ( 'NONE',  ( 0.7071067811865486830, -0.7071067811865464625, -0.000000000000000000 ) ) ;
#85096=ORIENTED_EDGE ( 'NONE', *, *, #45079, .T. ) ;
#85099=LINE ( 'NONE', #95967, #103127 ) ;
#85102=CARTESIAN_POINT ( 'NONE',  ( 27.32816939922333432, 11.25929247661560950, 4.000000000000000000 ) ) ;
#85103=DIRECTION ( 'NONE',  ( -0.7071067811865487940, 0.7071067811865463515, 0.000000000000000000 ) ) ;
#85104=CARTESIAN_POINT ( 'NONE',  ( 2.999999999999983569, -0.4125381241607568028, 4.000000000000000000 ) ) ;
#85105=VERTEX_POINT ( 'NONE', #50071 ) ;
#85108=ADVANCED_FACE ( 'NONE', ( #138501 ), #37033, .F. ) ;
#85111=DIRECTION ( 'NONE',  ( -0.000000000000000000, 0.000000000000000000, 1.000000000000000000 ) ) ;
#85112=CARTESIAN_POINT ( 'NONE',  ( -57.18398860626899705, 28.73617430169827358, 5.000000000000000000 ) ) ;
#85113=DIRECTION ( 'NONE',  ( 1.000000000000000000, 0.000000000000000000, 0.000000000000000000 ) ) ;
#85114=ORIENTED_EDGE ( 'NONE', *, *, #131351, .F. ) ;
#85115=ORIENTED_EDGE ( 'NONE', *, *, #33104, .T. ) ;
#85116=DIRECTION ( 'NONE',  ( 0.3543493200069162685, -0.000000000000000000, -0.9351131265310288487 ) ) ;
#85117=EDGE_CURVE ( 'NONE', #69618, #42560, #39188, .T. ) ;
#85118=ORIENTED_EDGE ( 'NONE', *, *, #1478, .T. ) ;
#85119=ORIENTED_EDGE ( 'NONE', *, *, #13618, .F. ) ;
#85121=DIRECTION ( 'NONE',  ( -0.6830127018922180770, -0.6830127018922204085, -0.2588190451025213501 ) ) ;
#85124=PLANE ( 'NONE',  #75735 ) ;
#85126=PLANE ( 'NONE',  #4784 ) ;
#85127=VECTOR ( 'NONE', #80173, 1000.000000000000000 ) ;
#85128=FACE_BOUND ( 'NONE', #31637, .T. ) ;
#85129=CARTESIAN_POINT ( 'NONE',  ( -10.77325839282159592, -11.24070752338416135, 18.24660765846980226 ) ) ;
#85131=CARTESIAN_POINT ( 'NONE',  ( -2.186508646023597624, -15.74070752338412760, 8.904080028138945835 ) ) ;
#85133=ORIENTED_EDGE ( 'NONE', *, *, #24714, .T. ) ;
#85134=AXIS2_PLACEMENT_3D ( 'NONE', #126847, #40592, #29678 ) ;
#85135=VECTOR ( 'NONE', #40073, 1000.000000000000227 ) ;
#85137=ORIENTED_EDGE ( 'NONE', *, *, #26978, .T. ) ;
#85138=EDGE_CURVE ( 'NONE', #78369, #125176, #4333, .T. ) ;
#85139=EDGE_LOOP ( 'NONE', ( #113728, #8368, #92478, #48992 ) ) ;
#85144=DIRECTION ( 'NONE',  ( 0.7071067811865486830, -0.7071067811865464625, -0.000000000000000000 ) ) ;
#85145=DIRECTION ( 'NONE',  ( 0.7071067811865487940, 0.7071067811865463515, 0.000000000000000000 ) ) ;
#85146=CARTESIAN_POINT ( 'NONE',  ( 24.18398860626899705, 28.73617430169804265, 5.000000000000000000 ) ) ;
#85147=DIRECTION ( 'NONE',  ( 0.7071067811865487940, -0.7071067811865463515, 0.000000000000000000 ) ) ;
#85149=PLANE ( 'NONE',  #32359 ) ;
#85150=CARTESIAN_POINT ( 'NONE',  ( 0.000000000000000000, 0.000000000000000000, 5.000000000000000000 ) ) ;
#85151=ORIENTED_EDGE ( 'NONE', *, *, #142880, .T. ) ;
#85152=CARTESIAN_POINT ( 'NONE',  ( -28.49999999999980460, -8.568876922607733704, 4.000000000000000000 ) ) ;
#85155=EDGE_LOOP ( 'NONE', ( #51518, #29053, #115908, #121309 ) ) ;
#85156=VERTEX_POINT ( 'NONE', #48635 ) ;
#85157=VERTEX_POINT ( 'NONE', #3648 ) ;
#85159=VECTOR ( 'NONE', #78395, 1000.000000000000000 ) ;
#85160=ORIENTED_EDGE ( 'NONE', *, *, #19415, .T. ) ;
#85164=EDGE_LOOP ( 'NONE', ( #133800, #42583, #119623, #43973, #85563 ) ) ;
#85165=DIRECTION ( 'NONE',  ( 0.3543493200069162685, -0.000000000000000000, -0.9351131265310288487 ) ) ;
#85166=ORIENTED_EDGE ( 'NONE', *, *, #59628, .T. ) ;
#85167=CARTESIAN_POINT ( 'NONE',  ( 22.82816939922337340, 9.759292476615614831, 4.000000000000000000 ) ) ;
#85168=DIRECTION ( 'NONE',  ( -0.7071067811865487940, 0.7071067811865463515, 0.000000000000000000 ) ) ;
#85169=DIRECTION ( 'NONE',  ( -0.3543493200069162685, -0.000000000000000000, -0.9351131265310288487 ) ) ;
#85171=ORIENTED_EDGE ( 'NONE', *, *, #74189, .T. ) ;
#85173=CARTESIAN_POINT ( 'NONE',  ( -4.809818324255480171, -18.74070752338408852, 7.910009926591521356 ) ) ;
#85174=ORIENTED_EDGE ( 'NONE', *, *, #46855, .T. ) ;
#85175=DIRECTION ( 'NONE',  ( -0.7071067811865486830, -0.7071067811865464625, -0.000000000000000000 ) ) ;
#85176=EDGE_LOOP ( 'NONE', ( #117734, #75687, #137688, #30824 ) ) ;
#85177=ORIENTED_EDGE ( 'NONE', *, *, #5956, .T. ) ;
#85178=ORIENTED_EDGE ( 'NONE', *, *, #135104, .F. ) ;
#85180=CYLINDRICAL_SURFACE ( 'NONE', #72359, 0.5000000000000004441 ) ;
#85181=LINE ( 'NONE', #130151, #95443 ) ;
#85182=EDGE_CURVE ( 'NONE', #9777, #44135, #137796, .T. ) ;
#85184=CARTESIAN_POINT ( 'NONE',  ( -21.72281430457044493, -21.72500000000000142, 5.000000000000000000 ) ) ;
#85185=CARTESIAN_POINT ( 'NONE',  ( -34.42500000000001137, -4.458600742197945443, 5.000000000000000000 ) ) ;
#85186=EDGE_CURVE ( 'NONE', #56636, #874, #15952, .T. ) ;
#85187=EDGE_CURVE ( 'NONE', #121799, #118878, #37773, .T. ) ;
#85188=ORIENTED_EDGE ( 'NONE', *, *, #31553, .F. ) ;
#85189=DIRECTION ( 'NONE',  ( -0.000000000000000000, 0.3543493200069153248, 0.9351131265310292928 ) ) ;
#85190=ORIENTED_EDGE ( 'NONE', *, *, #9462, .F. ) ;
#85191=CARTESIAN_POINT ( 'NONE',  ( 60.48921356237309510, -27.52281430457097500, 5.000000000000000000 ) ) ;
#85192=ADVANCED_FACE ( 'NONE', ( #27569 ), #116002, .T. ) ;
#85195=ORIENTED_EDGE ( 'NONE', *, *, #73955, .F. ) ;
#85196=LINE ( 'NONE', #129417, #69207 ) ;
#85197=VECTOR ( 'NONE', #7400, 1000.000000000000000 ) ;
#85198=LINE ( 'NONE', #30107, #60617 ) ;
#85200=ORIENTED_EDGE ( 'NONE', *, *, #82342, .T. ) ;
#85201=EDGE_CURVE ( 'NONE', #30701, #91520, #119559, .T. ) ;
#85202=DIRECTION ( 'NONE',  ( -0.7071067811865487940, 0.7071067811865463515, -0.000000000000000000 ) ) ;
#85203=LINE ( 'NONE', #30111, #106715 ) ;
#85204=PLANE ( 'NONE',  #81755 ) ;
#85205=DIRECTION ( 'NONE',  ( -0.000000000000000000, -0.3543493200069153248, -0.9351131265310291818 ) ) ;
#85207=CARTESIAN_POINT ( 'NONE',  ( -4.628234450443816428, -8.240707523384200428, 11.38925528200753590 ) ) ;
#85208=EDGE_CURVE ( 'NONE', #51865, #72597, #7953, .T. ) ;
#85209=FACE_OUTER_BOUND ( 'NONE', #49168, .T. ) ;
#85211=CARTESIAN_POINT ( 'NONE',  ( 26.99451991528749417, 28.92564299267956685, 4.000000000000000000 ) ) ;
#85212=EDGE_LOOP ( 'NONE', ( #125718, #28913, #42666, #67515 ) ) ;
#85213=DIRECTION ( 'NONE',  ( -0.6830127018922180770, -0.6830127018922204085, -0.2588190451025213501 ) ) ;
#85216=CARTESIAN_POINT ( 'NONE',  ( -5.510786437626906675, -27.52281430457051314, 5.000000000000000000 ) ) ;
#85217=ORIENTED_EDGE ( 'NONE', *, *, #47757, .F. ) ;
#85220=CARTESIAN_POINT ( 'NONE',  ( -34.92500000000001137, -18.18334561358938473, 4.500000000000000888 ) ) ;
#85221=VERTEX_POINT ( 'NONE', #6494 ) ;
#85222=VECTOR ( 'NONE', #47402, 1000.000000000000000 ) ;
#85224=LINE ( 'NONE', #86687, #10133 ) ;
#85225=VERTEX_POINT ( 'NONE', #18837 ) ;
#85226=VERTEX_POINT ( 'NONE', #118132 ) ;
#85230=ADVANCED_FACE ( 'NONE', ( #31873 ), #63108, .T. ) ;
#85231=VECTOR ( 'NONE', #72744, 1000.000000000000000 ) ;
#85232=VECTOR ( 'NONE', #39896, 1000.000000000000000 ) ;
#85235=PLANE ( 'NONE',  #18448 ) ;
#85236=LINE ( 'NONE', #121439, #27492 ) ;
#85237=ORIENTED_EDGE ( 'NONE', *, *, #10721, .T. ) ;
#85238=CARTESIAN_POINT ( 'NONE',  ( -33.18398860626899705, 28.73617430169810305, 5.000000000000000000 ) ) ;
#85239=CARTESIAN_POINT ( 'NONE',  ( 23.99999999999983658, -6.412538124160691133, 4.000000000000000000 ) ) ;
#85244=EDGE_CURVE ( 'NONE', #94538, #42016, #105831, .T. ) ;
#85245=ORIENTED_EDGE ( 'NONE', *, *, #118777, .T. ) ;
#85247=EDGE_CURVE ( 'NONE', #142848, #80772, #142088, .T. ) ;
#85248=PLANE ( 'NONE',  #75580 ) ;
#85249=CARTESIAN_POINT ( 'NONE',  ( -26.29387692260786125, 22.22500000000000142, 4.000000000000000000 ) ) ;
#85250=ORIENTED_EDGE ( 'NONE', *, *, #58773, .F. ) ;
#85251=CARTESIAN_POINT ( 'NONE',  ( -15.51665438641034989, 22.22500000000000142, 4.500000000000000888 ) ) ;
#85252=VECTOR ( 'NONE', #68490, 1000.000000000000000 ) ;
#85253=ADVANCED_FACE ( 'NONE', ( #117419 ), #96375, .T. ) ;
#85254=CARTESIAN_POINT ( 'NONE',  ( -27.18398860626900060, 28.73617430169806042, 5.000000000000000000 ) ) ;
#85255=CARTESIAN_POINT ( 'NONE',  ( -8.999999999999936051, -18.41253812416056235, 4.000000000000000000 ) ) ;
#85256=DIRECTION ( 'NONE',  ( -0.7071067811865486830, 0.7071067811865464625, 0.000000000000000000 ) ) ;
#85257=VERTEX_POINT ( 'NONE', #97846 ) ;
#85259=DIRECTION ( 'NONE',  ( -0.3543493200069162685, -0.000000000000000000, -0.9351131265310288487 ) ) ;
#85260=ADVANCED_FACE ( 'NONE', ( #30452 ), #42055, .F. ) ;
#85263=EDGE_LOOP ( 'NONE', ( #56869, #101376, #34986, #32358 ) ) ;
#85266=ORIENTED_EDGE ( 'NONE', *, *, #116135, .T. ) ;
#85267=EDGE_CURVE ( 'NONE', #42437, #106359, #139946, .T. ) ;
#85268=CARTESIAN_POINT ( 'NONE',  ( 7.499999999999951150, 1.030536316426518884, -5.498701923753815279 ) ) ;
#85269=CARTESIAN_POINT ( 'NONE',  ( -5.671830600776424092, -6.740707523384212863, 4.000000000000000000 ) ) ;
#85270=CARTESIAN_POINT ( 'NONE',  ( 24.55388970886357569, 5.485012786255876627, 4.000000000000000000 ) ) ;
#85272=ORIENTED_EDGE ( 'NONE', *, *, #58193, .T. ) ;
#85273=VECTOR ( 'NONE', #53622, 1000.000000000000227 ) ;
#85274=DIRECTION ( 'NONE',  ( 0.7071067811865487940, 0.7071067811865463515, -0.000000000000000000 ) ) ;
#85277=ORIENTED_EDGE ( 'NONE', *, *, #102150, .T. ) ;
#85278=DIRECTION ( 'NONE',  ( -0.000000000000000000, -0.3543493200069152693, 0.9351131265310292928 ) ) ;
#85280=DIRECTION ( 'NONE',  ( 0.7071067811865487940, 0.7071067811865463515, -0.000000000000000000 ) ) ;
#85281=ORIENTED_EDGE ( 'NONE', *, *, #43186, .F. ) ;
#85282=ORIENTED_EDGE ( 'NONE', *, *, #85374, .T. ) ;
#85283=ADVANCED_FACE ( 'NONE', ( #94964 ), #75386, .F. ) ;
#85284=DIRECTION ( 'NONE',  ( 0.7071067811865487940, 0.7071067811865463515, 0.000000000000000000 ) ) ;
#85285=CARTESIAN_POINT ( 'NONE',  ( 8.671830600776411657, 11.25929247661560062, 4.000000000000000000 ) ) ;
#85286=LINE ( 'NONE', #74454, #7255 ) ;
#85289=CARTESIAN_POINT ( 'NONE',  ( 7.499999999999951150, 0.4497235411627525936, -5.599840258123523817 ) ) ;
#85291=VERTEX_POINT ( 'NONE', #9360 ) ;
#85292=ORIENTED_EDGE ( 'NONE', *, *, #29937, .F. ) ;
#85294=ORIENTED_EDGE ( 'NONE', *, *, #45630, .F. ) ;
#85296=ADVANCED_FACE ( 'NONE', ( #7226 ), #86966, .T. ) ;
#85297=CARTESIAN_POINT ( 'NONE',  ( -20.29289321881331531, 14.25929247661557042, 5.000000000000000000 ) ) ;
#85298=PLANE ( 'NONE',  #28571 ) ;
#85299=EDGE_CURVE ( 'NONE', #18953, #67945, #129748, .T. ) ;
#85301=CARTESIAN_POINT ( 'NONE',  ( 34.49999999999975842, -19.53574439159931231, 4.994342998332164107 ) ) ;
#85302=CARTESIAN_POINT ( 'NONE',  ( 15.48921356237309510, -27.52281430457066236, 5.000000000000000000 ) ) ;
#85303=VECTOR ( 'NONE', #69002, 1000.000000000000000 ) ;
#85304=DIRECTION ( 'NONE',  ( 0.7071067811865486830, -0.7071067811865464625, -0.000000000000000000 ) ) ;
#85305=LINE ( 'NONE', #84624, #131809 ) ;
#85307=VECTOR ( 'NONE', #80763, 999.9999999999998863 ) ;
#85309=VECTOR ( 'NONE', #99364, 1000.000000000000227 ) ;
#85311=DIRECTION ( 'NONE',  ( 0.6830127018922180770, -0.6830127018922204085, -0.2588190451025214056 ) ) ;
#85313=VECTOR ( 'NONE', #89582, 999.9999999999998863 ) ;
#85314=ORIENTED_EDGE ( 'NONE', *, *, #138454, .F. ) ;
#85316=VERTEX_POINT ( 'NONE', #74690 ) ;
#85317=ADVANCED_FACE ( 'NONE', ( #107963 ), #73953, .F. ) ;
#85318=AXIS2_PLACEMENT_3D ( 'NONE', #117274, #31028, #20109 ) ;
#85319=CARTESIAN_POINT ( 'NONE',  ( -34.92500000000001137, -22.22500000000000142, 4.000000000000000000 ) ) ;
#85320=VERTEX_POINT ( 'NONE', #23098 ) ;
#85322=VECTOR ( 'NONE', #93555, 999.9999999999998863 ) ;
#85323=VERTEX_POINT ( 'NONE', #132655 ) ;
#85324=EDGE_LOOP ( 'NONE', ( #53011, #60136, #23014, #37777 ) ) ;
#85325=VECTOR ( 'NONE', #112675, 1000.000000000000000 ) ;
#85326=CARTESIAN_POINT ( 'NONE',  ( -30.72281430457039875, -21.72499999999999432, 5.000000000000000000 ) ) ;
#85327=LINE ( 'NONE', #51306, #84361 ) ;
#85329=PLANE ( 'NONE',  #128158 ) ;
#85330=CARTESIAN_POINT ( 'NONE',  ( -14.99451991528749595, 28.92564299267948513, 4.000000000000000000 ) ) ;
#85331=LINE ( 'NONE', #52709, #18548 ) ;
#85332=CARTESIAN_POINT ( 'NONE',  ( -14.95136400821897205, -1.164498636767092865, 4.123993368336923204 ) ) ;
#85333=AXIS2_PLACEMENT_3D ( 'NONE', #18313, #48142, #3859 ) ;
#85334=CARTESIAN_POINT ( 'NONE',  ( 0.000000000000000000, 0.000000000000000000, 5.000000000000000000 ) ) ;
#85335=CARTESIAN_POINT ( 'NONE',  ( 28.36246187583882161, 22.22500000000000853, 4.000000000000000000 ) ) ;
#85337=ORIENTED_EDGE ( 'NONE', *, *, #38620, .F. ) ;
#85338=AXIS2_PLACEMENT_3D ( 'NONE', #82946, #116278, #61243 ) ;
#85339=CARTESIAN_POINT ( 'NONE',  ( 30.52400138585428024, 22.03583458319437938, 4.979811245910086726 ) ) ;
#85340=VERTEX_POINT ( 'NONE', #121711 ) ;
#85341=ORIENTED_EDGE ( 'NONE', *, *, #8422, .F. ) ;
#85342=ORIENTED_EDGE ( 'NONE', *, *, #139666, .T. ) ;
#85343=AXIS2_PLACEMENT_3D ( 'NONE', #78468, #122659, #34977 ) ;
#85345=VECTOR ( 'NONE', #87775, 1000.000000000000000 ) ;
#85346=VECTOR ( 'NONE', #26572, 1000.000000000000000 ) ;
#85348=DIRECTION ( 'NONE',  ( 0.7071067811865487940, 0.7071067811865463515, 0.000000000000000000 ) ) ;
#85350=CARTESIAN_POINT ( 'NONE',  ( 42.48921356237308800, -27.52281430457085065, 5.000000000000000000 ) ) ;
#85351=EDGE_CURVE ( 'NONE', #19753, #64278, #90548, .T. ) ;
#85352=ORIENTED_EDGE ( 'NONE', *, *, #104428, .F. ) ;
#85354=ORIENTED_EDGE ( 'NONE', *, *, #38711, .T. ) ;
#85355=VECTOR ( 'NONE', #3544, 1000.000000000000000 ) ;
#85356=VECTOR ( 'NONE', #94243, 1000.000000000000000 ) ;
#85357=EDGE_CURVE ( 'NONE', #45681, #113219, #110124, .T. ) ;
#85361=DIRECTION ( 'NONE',  ( 0.6830127018922180770, -0.6830127018922204085, -0.2588190451025213501 ) ) ;
#85362=PLANE ( 'NONE',  #320 ) ;
#85363=ORIENTED_EDGE ( 'NONE', *, *, #143104, .T. ) ;
#85364=ORIENTED_EDGE ( 'NONE', *, *, #99630, .F. ) ;
#85365=EDGE_CURVE ( 'NONE', #75031, #119204, #11506, .T. ) ;
#85366=ORIENTED_EDGE ( 'NONE', *, *, #90345, .F. ) ;
#85368=CARTESIAN_POINT ( 'NONE',  ( -4.433128002487388919, -21.74070752338405299, 6.915939825044087108 ) ) ;
#85369=DIRECTION ( 'NONE',  ( 0.3543493200069162685, -0.000000000000000000, -0.9351131265310288487 ) ) ;
#85370=VECTOR ( 'NONE', #47464, 1000.000000000000000 ) ;
#85371=EDGE_CURVE ( 'NONE', #24456, #77699, #112301, .T. ) ;
#85372=CARTESIAN_POINT ( 'NONE',  ( -27.32816939922334143, -3.740707523384241728, 4.000000000000000000 ) ) ;
#85373=CARTESIAN_POINT ( 'NONE',  ( -34.92500000000001137, -22.22500000000000142, 4.000000000000000000 ) ) ;
#85374=EDGE_CURVE ( 'NONE', #45102, #79366, #2051, .T. ) ;
#85375=CARTESIAN_POINT ( 'NONE',  ( 23.12514619309220976, -14.24070752338412937, 9.401115078912607004 ) ) ;
#85379=VERTEX_POINT ( 'NONE', #65965 ) ;
#85380=DIRECTION ( 'NONE',  ( 0.7071067811865487940, 0.7071067811865463515, 0.000000000000000000 ) ) ;
#85381=PLANE ( 'NONE',  #37830 ) ;
#85382=ORIENTED_EDGE ( 'NONE', *, *, #88302, .F. ) ;
#85383=EDGE_CURVE ( 'NONE', #22682, #143327, #44945, .T. ) ;
#85384=LINE ( 'NONE', #74548, #39122 ) ;
#85386=ORIENTED_EDGE ( 'NONE', *, *, #47220, .F. ) ;
#85387=PLANE ( 'NONE',  #14423 ) ;
#85388=CARTESIAN_POINT ( 'NONE',  ( 2.510786437626908008, -27.52281430457053446, 5.000000000000000000 ) ) ;
#85389=ORIENTED_EDGE ( 'NONE', *, *, #9795, .T. ) ;
#85390=DIRECTION ( 'NONE',  ( -0.7071067811865486830, -0.7071067811865464625, 0.000000000000000000 ) ) ;
#85391=ORIENTED_EDGE ( 'NONE', *, *, #46958, .F. ) ;
#85392=EDGE_CURVE ( 'NONE', #108519, #23652, #142772, .T. ) ;
#85393=PLANE ( 'NONE',  #59104 ) ;
#85395=CARTESIAN_POINT ( 'NONE',  ( 28.49999999999980815, 16.46639925780209168, 5.000000000000000000 ) ) ;
#85396=DIRECTION ( 'NONE',  ( 1.000000000000000000, 0.000000000000000000, 0.000000000000000000 ) ) ;
#85398=LINE ( 'NONE', #129623, #87856 ) ;
#85401=DIRECTION ( 'NONE',  ( -0.7071067811865486830, -0.7071067811865464625, 0.000000000000000000 ) ) ;
#85402=CARTESIAN_POINT ( 'NONE',  ( 34.42499999999998295, 14.97718569542923994, 5.000000000000000000 ) ) ;
#85403=EDGE_LOOP ( 'NONE', ( #137988, #42581, #31411, #121593 ) ) ;
#85406=ORIENTED_EDGE ( 'NONE', *, *, #33742, .F. ) ;
#85407=EDGE_CURVE ( 'NONE', #126528, #48470, #87680, .T. ) ;
#85408=DIRECTION ( 'NONE',  ( -0.000000000000000000, -0.3543493200069152693, 0.9351131265310292928 ) ) ;
#85410=DIRECTION ( 'NONE',  ( -0.6830127018922180770, -0.6830127018922204085, -0.2588190451025213501 ) ) ;
#85411=VERTEX_POINT ( 'NONE', #76838 ) ;
#85412=AXIS2_PLACEMENT_3D ( 'NONE', #57719, #43974, #12741 ) ;
#85413=AXIS2_PLACEMENT_3D ( 'NONE', #114266, #101245, #135335 ) ;
#85415=DIRECTION ( 'NONE',  ( 0.6830127018922180770, -0.6830127018922204085, -0.2588190451025213501 ) ) ;
#85416=AXIS2_PLACEMENT_3D ( 'NONE', #7912, #41265, #118834 ) ;
#85418=CARTESIAN_POINT ( 'NONE',  ( -4.499999999999976019, -12.08601207473290451, -10.46905243149093678 ) ) ;
#85420=LINE ( 'NONE', #63714, #63724 ) ;
#85421=EDGE_LOOP ( 'NONE', ( #137818, #37124, #42527, #14396 ) ) ;
#85423=DIRECTION ( 'NONE',  ( 0.7071067811865486830, -0.7071067811865464625, -0.000000000000000000 ) ) ;
#85424=CARTESIAN_POINT ( 'NONE',  ( 26.99999999999981526, 10.55218569542905982, 5.000000000000000000 ) ) ;
#85425=DIRECTION ( 'NONE',  ( 0.6830127018922181881, 0.6830127018922202975, -0.2588190451025214056 ) ) ;
#85426=EDGE_CURVE ( 'NONE', #16634, #25329, #46364, .T. ) ;
#85427=DIRECTION ( 'NONE',  ( -0.7071067811865486830, -0.7071067811865464625, -0.000000000000000000 ) ) ;
#85428=EDGE_LOOP ( 'NONE', ( #130961, #126174, #4468, #107660 ) ) ;
#85429=ORIENTED_EDGE ( 'NONE', *, *, #95723, .F. ) ;
#85430=ORIENTED_EDGE ( 'NONE', *, *, #12935, .T. ) ;
#85433=EDGE_CURVE ( 'NONE', #86890, #125242, #88414, .T. ) ;
#85435=VECTOR ( 'NONE', #16749, 1000.000000000000227 ) ;
#85437=ORIENTED_EDGE ( 'NONE', *, *, #29230, .T. ) ;
#85440=VECTOR ( 'NONE', #95947, 1000.000000000000000 ) ;
#85443=EDGE_CURVE ( 'NONE', #108968, #20344, #12248, .T. ) ;
#85444=CARTESIAN_POINT ( 'NONE',  ( 34.98012225071431658, -17.24070752338409562, 20.23474786156477023 ) ) ;
#85445=DIRECTION ( 'NONE',  ( 0.6830127018922180770, -0.6830127018922204085, -0.2588190451025213501 ) ) ;
#85448=DIRECTION ( 'NONE',  ( 0.7071067811865487940, 0.7071067811865463515, 0.000000000000000000 ) ) ;
#85450=VECTOR ( 'NONE', #14952, 999.9999999999998863 ) ;
#85451=ORIENTED_EDGE ( 'NONE', *, *, #124396, .T. ) ;
#85452=ORIENTED_EDGE ( 'NONE', *, *, #121442, .T. ) ;
#85453=EDGE_CURVE ( 'NONE', #69350, #132873, #12949, .T. ) ;
#85454=EDGE_LOOP ( 'NONE', ( #40176, #89898, #4664, #25300 ) ) ;
#85455=LINE ( 'NONE', #97776, #116563 ) ;
#85458=AXIS2_PLACEMENT_3D ( 'NONE', #142662, #132537, #33228 ) ;
#85459=VECTOR ( 'NONE', #68630, 1000.000000000000000 ) ;
#85460=CARTESIAN_POINT ( 'NONE',  ( -28.49999999999980105, 3.653845994658365459, -4.504631822206305536 ) ) ;
#85461=ADVANCED_FACE ( 'NONE', ( #89809 ), #57224, .T. ) ;
#85462=ORIENTED_EDGE ( 'NONE', *, *, #7212, .T. ) ;
#85463=ORIENTED_EDGE ( 'NONE', *, *, #35822, .T. ) ;
#85464=CARTESIAN_POINT ( 'NONE',  ( -42.18398860626899705, 28.73617430169816700, 5.000000000000000000 ) ) ;
#85465=ORIENTED_EDGE ( 'NONE', *, *, #574, .T. ) ;
#85466=ORIENTED_EDGE ( 'NONE', *, *, #105519, .F. ) ;
#85467=VECTOR ( 'NONE', #78451, 1000.000000000000000 ) ;
#85468=ADVANCED_FACE ( 'NONE', ( #101402 ), #123184, .F. ) ;
#85469=LINE ( 'NONE', #128987, #127679 ) ;
#85470=DIRECTION ( 'NONE',  ( -0.7071067811865486830, 0.7071067811865464625, 0.000000000000000000 ) ) ;
#85471=EDGE_CURVE ( 'NONE', #141889, #114933, #65243, .T. ) ;
#85472=ORIENTED_EDGE ( 'NONE', *, *, #110757, .F. ) ;
#85474=CARTESIAN_POINT ( 'NONE',  ( -12.33010218547257786, 17.25929247661554555, 19.83885114516074211 ) ) ;
#85476=DIRECTION ( 'NONE',  ( 0.6830127018922181881, 0.6830127018922202975, -0.2588190451025214056 ) ) ;
#85478=ORIENTED_EDGE ( 'NONE', *, *, #108437, .F. ) ;
#85479=DIRECTION ( 'NONE',  ( -0.000000000000000000, 0.3543493200069152138, -0.9351131265310292928 ) ) ;
#85480=FACE_BOUND ( 'NONE', #63173, .T. ) ;
#85484=DIRECTION ( 'NONE',  ( 0.7071067811865487940, 0.7071067811865463515, -0.000000000000000000 ) ) ;
#85485=EDGE_CURVE ( 'NONE', #76457, #48400, #92656, .T. ) ;
#85486=ORIENTED_EDGE ( 'NONE', *, *, #38715, .T. ) ;
#85487=CARTESIAN_POINT ( 'NONE',  ( 22.13389675353461072, 22.22500000000000142, 26.62174895348230308 ) ) ;
#85488=VERTEX_POINT ( 'NONE', #47784 ) ;
#85489=ORIENTED_EDGE ( 'NONE', *, *, #93759, .F. ) ;
#85491=CARTESIAN_POINT ( 'NONE',  ( 0.000000000000000000, 0.000000000000000000, 5.000000000000000000 ) ) ;
#85492=CARTESIAN_POINT ( 'NONE',  ( 19.88982677111775033, -22.22500000000000142, 4.785647885939350310 ) ) ;
#85493=DIRECTION ( 'NONE',  ( 0.6830127018922180770, -0.6830127018922204085, -0.2588190451025213501 ) ) ;
#85495=DIRECTION ( 'NONE',  ( -0.7071067811865486830, -0.7071067811865464625, 0.000000000000000000 ) ) ;
#85496=DIRECTION ( 'NONE',  ( 0.7071067811865486830, -0.7071067811865464625, -0.000000000000000000 ) ) ;
#85497=CARTESIAN_POINT ( 'NONE',  ( 0.000000000000000000, 0.000000000000000000, 5.000000000000000000 ) ) ;
#85498=CARTESIAN_POINT ( 'NONE',  ( 30.70710678118633297, -0.7407075233842753681, 5.000000000000000000 ) ) ;
#85499=LINE ( 'NONE', #73241, #20465 ) ;
#85500=DIRECTION ( 'NONE',  ( 0.7071067811865486830, -0.7071067811865464625, -0.000000000000000000 ) ) ;
#85501=CARTESIAN_POINT ( 'NONE',  ( 12.79289321881336861, 3.759292476615681888, 5.000000000000000000 ) ) ;
#85502=EDGE_LOOP ( 'NONE', ( #95976, #26426, #42981, #74110 ) ) ;
#85503=EDGE_LOOP ( 'NONE', ( #55936, #602, #97550, #18090 ) ) ;
#85504=ORIENTED_EDGE ( 'NONE', *, *, #107044, .T. ) ;
#85505=EDGE_LOOP ( 'NONE', ( #24511, #27101, #57147, #129099 ) ) ;
#85506=DIRECTION ( 'NONE',  ( 0.7071067811865487940, 0.7071067811865463515, 0.000000000000000000 ) ) ;
#85507=VECTOR ( 'NONE', #50247, 1000.000000000000000 ) ;
#85509=ORIENTED_EDGE ( 'NONE', *, *, #142211, .T. ) ;
#85510=VECTOR ( 'NONE', #79284, 999.9999999999998863 ) ;
#85511=VECTOR ( 'NONE', #20051, 1000.000000000000000 ) ;
#85512=VERTEX_POINT ( 'NONE', #38304 ) ;
#85513=CARTESIAN_POINT ( 'NONE',  ( 12.18398860626900060, 28.73617430169795739, 5.000000000000000000 ) ) ;
#85515=DIRECTION ( 'NONE',  ( 0.7071067811865487940, 0.7071067811865463515, 0.000000000000000000 ) ) ;
#85516=VERTEX_POINT ( 'NONE', #103523 ) ;
#85517=DIRECTION ( 'NONE',  ( -0.6830127018922181881, 0.6830127018922202975, -0.2588190451025214056 ) ) ;
#85518=ORIENTED_EDGE ( 'NONE', *, *, #138877, .F. ) ;
#85519=FACE_BOUND ( 'NONE', #20977, .T. ) ;
#85521=ADVANCED_FACE ( 'NONE', ( #4163 ), #48455, .F. ) ;
#85524=VERTEX_POINT ( 'NONE', #24555 ) ;
#85526=DIRECTION ( 'NONE',  ( 0.7071067811865487940, 0.7071067811865463515, -0.000000000000000000 ) ) ;
#85527=EDGE_CURVE ( 'NONE', #373, #86911, #60065, .T. ) ;
#85528=CARTESIAN_POINT ( 'NONE',  ( -2.999999999999978240, -7.068876922607738145, 4.000000000000000000 ) ) ;
#85529=DIRECTION ( 'NONE',  ( -8.817971600062198362E-18, -0.3543493200069152693, 0.9351131265310292928 ) ) ;
#85530=VERTEX_POINT ( 'NONE', #79717 ) ;
#85531=VERTEX_POINT ( 'NONE', #81841 ) ;
#85532=ADVANCED_FACE ( 'NONE', ( #126034 ), #115813, .T. ) ;
#85534=ORIENTED_EDGE ( 'NONE', *, *, #71336, .F. ) ;
#85535=AXIS2_PLACEMENT_3D ( 'NONE', #1225, #67991, #33214 ) ;
#85536=CARTESIAN_POINT ( 'NONE',  ( 60.29974487139158867, -27.71228299555248142, 4.000000000000000000 ) ) ;
#85538=LINE ( 'NONE', #84171, #115902 ) ;
#85539=CARTESIAN_POINT ( 'NONE',  ( -1.499999999999994449, 1.030536316426501564, -5.498701923753798404 ) ) ;
#85540=EDGE_CURVE ( 'NONE', #68848, #93995, #91951, .T. ) ;
#85542=( BOUNDED_CURVE ( )  B_SPLINE_CURVE ( 3, ( #59689, #37200, #114736, #48092 ),
 .UNSPECIFIED., .F., .F. ) 
 B_SPLINE_CURVE_WITH_KNOTS ( ( 4, 4 ),
 ( 1.964434688349479652, 3.503810798801450854 ),
 .UNSPECIFIED. ) 
 CURVE ( )  GEOMETRIC_REPRESENTATION_ITEM ( )  RATIONAL_B_SPLINE_CURVE ( ( 1.000000000000000000, 0.8120851936182262865, 0.8120851936182262865, 1.000000000000000000 ) ) 
 REPRESENTATION_ITEM ( '' )  );
#85543=ORIENTED_EDGE ( 'NONE', *, *, #80512, .T. ) ;
#85545=VECTOR ( 'NONE', #70168, 1000.000000000000000 ) ;
#85546=LINE ( 'NONE', #129778, #139268 ) ;
#85548=EDGE_LOOP ( 'NONE', ( #50974, #124798, #135814, #64411 ) ) ;
#85549=LINE ( 'NONE', #129782, #83668 ) ;
#85550=VECTOR ( 'NONE', #100973, 1000.000000000000000 ) ;
#85551=CARTESIAN_POINT ( 'NONE',  ( 17.81601139373099940, 28.73617430169775133, 5.000000000000000000 ) ) ;
#85553=EDGE_LOOP ( 'NONE', ( #22144, #107467, #42611, #8300 ) ) ;
#85555=ADVANCED_FACE ( 'NONE', ( #49908 ), #3490, .F. ) ;
#85556=DIRECTION ( 'NONE',  ( 0.6830127018922181881, 0.6830127018922202975, -0.2588190451025214056 ) ) ;
#85557=ORIENTED_EDGE ( 'NONE', *, *, #121798, .T. ) ;
#85558=VERTEX_POINT ( 'NONE', #102852 ) ;
#85559=EDGE_CURVE ( 'NONE', #106514, #130620, #136175, .T. ) ;
#85560=CARTESIAN_POINT ( 'NONE',  ( -2.999999999999981792, -10.77435723561695902, -9.972017380717224100 ) ) ;
#85562=CARTESIAN_POINT ( 'NONE',  ( -48.18398860626899705, 28.73617430169820608, 5.000000000000000000 ) ) ;
#85563=ORIENTED_EDGE ( 'NONE', *, *, #140730, .F. ) ;
#85564=CARTESIAN_POINT ( 'NONE',  ( 11.70025512860841133, -27.71228299555198049, 4.000000000000000000 ) ) ;
#85565=ADVANCED_FACE ( 'NONE', ( #104968 ), #113712, .F. ) ;
#85566=CARTESIAN_POINT ( 'NONE',  ( 14.29289321881336683, -15.74070752338412404, 5.000000000000000000 ) ) ;
#85567=DIRECTION ( 'NONE',  ( -0.3543493200069162685, -0.000000000000000000, -0.9351131265310288487 ) ) ;
#85570=CARTESIAN_POINT ( 'NONE',  ( -22.49999999999984013, -7.420205493532918695, -2.617629953481305893 ) ) ;
#85572=CARTESIAN_POINT ( 'NONE',  ( 34.92499999999998295, -21.72500000000000142, 5.000000000000000000 ) ) ;
#85573=ADVANCED_FACE ( 'NONE', ( #126706 ), #70944, .F. ) ;
#85574=CARTESIAN_POINT ( 'NONE',  ( -26.20666063542134339, 21.75929247661549226, 4.998822639870711626 ) ) ;
#85575=AXIS2_PLACEMENT_3D ( 'NONE', #26746, #5684, #126080 ) ;
#85576=DIRECTION ( 'NONE',  ( 0.7071067811865487940, 0.7071067811865463515, -0.000000000000000000 ) ) ;
#85577=CARTESIAN_POINT ( 'NONE',  ( -6.328169399223483538, 17.25929247661554200, 4.000000000000000000 ) ) ;
#85578=CARTESIAN_POINT ( 'NONE',  ( -12.48921356237309155, -27.52281430457064104, 5.000000000000000000 ) ) ;
#85580=VERTEX_POINT ( 'NONE', #91278 ) ;
#85581=ORIENTED_EDGE ( 'NONE', *, *, #19747, .F. ) ;
#85582=VERTEX_POINT ( 'NONE', #80397 ) ;
#85584=ORIENTED_EDGE ( 'NONE', *, *, #5839, .T. ) ;
#85585=ORIENTED_EDGE ( 'NONE', *, *, #43186, .T. ) ;
#85586=VERTEX_POINT ( 'NONE', #4899 ) ;
#85587=ADVANCED_FACE ( 'NONE', ( #135488 ), #59366, .F. ) ;
#85588=CARTESIAN_POINT ( 'NONE',  ( -17.70025512860841488, -27.71228299555193786, 4.000000000000000000 ) ) ;
#85590=ORIENTED_EDGE ( 'NONE', *, *, #53136, .T. ) ;
#85591=DIRECTION ( 'NONE',  ( -0.6830127018922180770, -0.6830127018922204085, -0.2588190451025213501 ) ) ;
#85592=LINE ( 'NONE', #129829, #78774 ) ;
#85593=LINE ( 'NONE', #142850, #85738 ) ;
#85596=EDGE_LOOP ( 'NONE', ( #137513, #108578, #73422, #111144 ) ) ;
#85598=LINE ( 'NONE', #108047, #1069 ) ;
#85599=DIRECTION ( 'NONE',  ( -0.000000000000000000, 0.000000000000000000, 1.000000000000000000 ) ) ;
#85601=FACE_OUTER_BOUND ( 'NONE', #94117, .T. ) ;
#85606=ORIENTED_EDGE ( 'NONE', *, *, #62139, .T. ) ;
#85607=ORIENTED_EDGE ( 'NONE', *, *, #114496, .T. ) ;
#85609=ORIENTED_EDGE ( 'NONE', *, *, #43837, .F. ) ;
#85610=LINE ( 'NONE', #108059, #141241 ) ;
#85611=ADVANCED_FACE ( 'NONE', ( #112988 ), #104235, .F. ) ;
#85612=DIRECTION ( 'NONE',  ( -0.7071067811865487940, 0.7071067811865463515, 0.000000000000000000 ) ) ;
#85614=DIRECTION ( 'NONE',  ( 0.7071067811865487940, 0.7071067811865463515, 0.000000000000000000 ) ) ;
#85615=CARTESIAN_POINT ( 'NONE',  ( 42.18398860626899705, 28.73617430169816700, 5.000000000000000000 ) ) ;
#85619=ADVANCED_FACE ( 'NONE', ( #102142 ), #2798, .T. ) ;
#85620=LINE ( 'NONE', #28419, #78034 ) ;
#85622=DIRECTION ( 'NONE',  ( -0.6830127018922180770, -0.6830127018922204085, -0.2588190451025213501 ) ) ;
#85623=VECTOR ( 'NONE', #71839, 999.9999999999998863 ) ;
#85624=VECTOR ( 'NONE', #38153, 1000.000000000000000 ) ;
#85625=VECTOR ( 'NONE', #43487, 1000.000000000000000 ) ;
#85626=CARTESIAN_POINT ( 'NONE',  ( 71.99451991528749772, 28.92564299267988304, 4.000000000000000000 ) ) ;
#85627=DIRECTION ( 'NONE',  ( 0.3543493200069163240, 0.000000000000000000, 0.9351131265310288487 ) ) ;
#85628=AXIS2_PLACEMENT_3D ( 'NONE', #117750, #62717, #129364 ) ;
#85629=CARTESIAN_POINT ( 'NONE',  ( 29.21837311707485085, 21.74787736706806385, 4.999607392498049308 ) ) ;
#85632=EDGE_CURVE ( 'NONE', #91948, #40577, #17252, .T. ) ;
#85633=VERTEX_POINT ( 'NONE', #86091 ) ;
#85635=LINE ( 'NONE', #75499, #101712 ) ;
#85636=LINE ( 'NONE', #118991, #98785 ) ;
#85637=CARTESIAN_POINT ( 'NONE',  ( 30.18398860626900060, 28.73617430169808173, 5.000000000000000000 ) ) ;
#85640=ORIENTED_EDGE ( 'NONE', *, *, #57493, .T. ) ;
#85641=EDGE_CURVE ( 'NONE', #22050, #108173, #107106, .T. ) ;
#85642=DIRECTION ( 'NONE',  ( 0.7071067811865486830, -0.7071067811865464625, -0.000000000000000000 ) ) ;
#85643=ORIENTED_EDGE ( 'NONE', *, *, #15169, .F. ) ;
#85644=ORIENTED_EDGE ( 'NONE', *, *, #32868, .F. ) ;
#85646=ORIENTED_EDGE ( 'NONE', *, *, #115572, .T. ) ;
#85649=EDGE_CURVE ( 'NONE', #53505, #135463, #61513, .T. ) ;
#85650=ORIENTED_EDGE ( 'NONE', *, *, #69240, .T. ) ;
#85651=DIRECTION ( 'NONE',  ( -0.7071067811865487940, 0.7071067811865463515, 0.000000000000000000 ) ) ;
#85652=FACE_OUTER_BOUND ( 'NONE', #103435, .T. ) ;
#85653=AXIS2_PLACEMENT_3D ( 'NONE', #26771, #17995, #128245 ) ;
#85654=CARTESIAN_POINT ( 'NONE',  ( 0.000000000000000000, 0.000000000000000000, 5.000000000000000000 ) ) ;
#85655=EDGE_CURVE ( 'NONE', #46033, #123098, #7782, .T. ) ;
#85656=FACE_BOUND ( 'NONE', #39973, .T. ) ;
#85657=EDGE_LOOP ( 'NONE', ( #124352, #132514, #53383, #63468 ) ) ;
#85658=FACE_OUTER_BOUND ( 'NONE', #58917, .T. ) ;
#85660=CARTESIAN_POINT ( 'NONE',  ( -10.49999999999992539, -19.53360074219753884, 5.000000000000000000 ) ) ;
#85662=EDGE_CURVE ( 'NONE', #53640, #47010, #116567, .T. ) ;
#85663=ORIENTED_EDGE ( 'NONE', *, *, #115749, .F. ) ;
#85664=DIRECTION ( 'NONE',  ( -0.7071067811865487940, 0.7071067811865463515, -0.000000000000000000 ) ) ;
#85665=ORIENTED_EDGE ( 'NONE', *, *, #77083, .F. ) ;
#85666=AXIS2_PLACEMENT_3D ( 'NONE', #27668, #4423, #137889 ) ;
#85667=ORIENTED_EDGE ( 'NONE', *, *, #73548, .F. ) ;
#85668=CARTESIAN_POINT ( 'NONE',  ( -24.08491323193747036, -12.74070752338414891, 18.74364270924348830 ) ) ;
#85669=ORIENTED_EDGE ( 'NONE', *, *, #55165, .T. ) ;
#85671=VERTEX_POINT ( 'NONE', #72399 ) ;
#85672=VECTOR ( 'NONE', #114718, 1000.000000000000000 ) ;
#85673=PLANE ( 'NONE',  #71943 ) ;
#85674=FACE_OUTER_BOUND ( 'NONE', #53445, .T. ) ;
#85675=ORIENTED_EDGE ( 'NONE', *, *, #47312, .F. ) ;
#85676=CARTESIAN_POINT ( 'NONE',  ( 75.29974487139158157, -27.71228299555258445, 4.000000000000000000 ) ) ;
#85677=VECTOR ( 'NONE', #85059, 1000.000000000000000 ) ;
#85678=EDGE_CURVE ( 'NONE', #26874, #123294, #30271, .T. ) ;
#85679=LINE ( 'NONE', #32029, #138205 ) ;
#85680=LINE ( 'NONE', #98702, #20406 ) ;
#85681=CARTESIAN_POINT ( 'NONE',  ( -14.21837311707495743, 21.74787736706806385, 4.999607392498048419 ) ) ;
#85682=LINE ( 'NONE', #141515, #30901 ) ;
#85683=DIRECTION ( 'NONE',  ( -0.7071067811865487940, 0.7071067811865463515, -0.000000000000000000 ) ) ;
#85684=ORIENTED_EDGE ( 'NONE', *, *, #44495, .T. ) ;
#85685=VECTOR ( 'NONE', #85881, 1000.000000000000227 ) ;
#85686=ORIENTED_EDGE ( 'NONE', *, *, #68813, .T. ) ;
#85687=LINE ( 'NONE', #131355, #100653 ) ;
#85688=PLANE ( 'NONE',  #25803 ) ;
#85690=VERTEX_POINT ( 'NONE', #62931 ) ;
#85691=ORIENTED_EDGE ( 'NONE', *, *, #93745, .T. ) ;
#85692=CARTESIAN_POINT ( 'NONE',  ( -26.58838509405149964, 22.22500000000000142, 4.777194822843817690 ) ) ;
#85693=PLANE ( 'NONE',  #105837 ) ;
#85694=CARTESIAN_POINT ( 'NONE',  ( 9.005480084712511157, 28.92564299267931816, 4.000000000000000000 ) ) ;
#85695=ORIENTED_EDGE ( 'NONE', *, *, #512, .F. ) ;
#85696=CARTESIAN_POINT ( 'NONE',  ( -0.7071067811865329178, -18.74070752338408852, 5.000000000000000000 ) ) ;
#85697=VECTOR ( 'NONE', #70819, 1000.000000000000000 ) ;
#85698=LINE ( 'NONE', #30646, #5298 ) ;
#85700=EDGE_CURVE ( 'NONE', #42461, #18783, #18656, .T. ) ;
#85702=ORIENTED_EDGE ( 'NONE', *, *, #138609, .T. ) ;
#85705=ADVANCED_FACE ( 'NONE', ( #6321 ), #106363, .F. ) ;
#85706=CARTESIAN_POINT ( 'NONE',  ( -34.42500000000001137, 22.22500000000000142, 5.000000000000000000 ) ) ;
#85707=FACE_OUTER_BOUND ( 'NONE', #44958, .T. ) ;
#85708=DIRECTION ( 'NONE',  ( 0.7071067811865487940, -0.7071067811865463515, 0.000000000000000000 ) ) ;
#85710=DIRECTION ( 'NONE',  ( 0.7071067811865487940, 0.7071067811865463515, 0.000000000000000000 ) ) ;
#85711=EDGE_LOOP ( 'NONE', ( #101747, #48327, #125556, #111300 ) ) ;
#85714=CYLINDRICAL_SURFACE ( 'NONE', #118719, 0.5000000000000004441 ) ;
#85716=EDGE_CURVE ( 'NONE', #40019, #44445, #41875, .T. ) ;
#85717=DIRECTION ( 'NONE',  ( 0.3543493200069162685, -0.000000000000000000, -0.9351131265310288487 ) ) ;
#85719=AXIS2_PLACEMENT_3D ( 'NONE', #26832, #39890, #17383 ) ;
#85720=VECTOR ( 'NONE', #69526, 999.9999999999998863 ) ;
#85721=DIRECTION ( 'NONE',  ( -0.7071067811865487940, 0.7071067811865463515, 0.000000000000000000 ) ) ;
#85722=CARTESIAN_POINT ( 'NONE',  ( -25.49999999999981526, 19.46639925780206326, 5.000000000000000000 ) ) ;
#85724=ORIENTED_EDGE ( 'NONE', *, *, #54320, .T. ) ;
#85725=VECTOR ( 'NONE', #86968, 1000.000000000000227 ) ;
#85726=VECTOR ( 'NONE', #89843, 1000.000000000000000 ) ;
#85727=VECTOR ( 'NONE', #117270, 999.9999999999998863 ) ;
#85728=CARTESIAN_POINT ( 'NONE',  ( -25.00193056682080339, -22.22500000000000142, 4.500000000000000888 ) ) ;
#85730=CARTESIAN_POINT ( 'NONE',  ( 0.7228143045705931469, -21.72500000000000142, 5.000000000000000000 ) ) ;
#85731=VECTOR ( 'NONE', #7768, 1000.000000000000000 ) ;
#85732=DIRECTION ( 'NONE',  ( -0.7071067811865486830, -0.7071067811865464625, -0.000000000000000000 ) ) ;
#85733=ADVANCED_FACE ( 'NONE', ( #39011 ), #75232, .T. ) ;
#85735=EDGE_CURVE ( 'NONE', #81832, #23063, #128179, .T. ) ;
#85736=ORIENTED_EDGE ( 'NONE', *, *, #121765, .F. ) ;
#85737=CARTESIAN_POINT ( 'NONE',  ( 21.00548008471250938, 28.92564299267923644, 4.000000000000000000 ) ) ;
#85738=VECTOR ( 'NONE', #141423, 1000.000000000000227 ) ;
#85739=LINE ( 'NONE', #42271, #136265 ) ;
#85742=DIRECTION ( 'NONE',  ( -0.000000000000000000, 0.3543493200069153248, 0.9351131265310292928 ) ) ;
#85743=FACE_OUTER_BOUND ( 'NONE', #67103, .T. ) ;
#85744=CARTESIAN_POINT ( 'NONE',  ( -3.005480084712505828, 28.92564299267936079, 4.000000000000000000 ) ) ;
#85745=ORIENTED_EDGE ( 'NONE', *, *, #57047, .T. ) ;
#85747=DIRECTION ( 'NONE',  ( 0.7071067811865486830, -0.7071067811865464625, -0.000000000000000000 ) ) ;
#85749=VECTOR ( 'NONE', #94115, 999.9999999999998863 ) ;
#85750=ADVANCED_FACE ( 'NONE', ( #127440 ), #29538, .F. ) ;
#85754=VECTOR ( 'NONE', #108073, 1000.000000000000000 ) ;
#85755=ORIENTED_EDGE ( 'NONE', *, *, #131259, .T. ) ;
#85759=VECTOR ( 'NONE', #32859, 1000.000000000000000 ) ;
#85761=EDGE_CURVE ( 'NONE', #14566, #139810, #83231, .T. ) ;
#85762=DIRECTION ( 'NONE',  ( -0.3543493200069162685, -0.000000000000000000, -0.9351131265310288487 ) ) ;
#85763=DIRECTION ( 'NONE',  ( 0.7071067811865486830, -0.7071067811865464625, -0.000000000000000000 ) ) ;
#85765=EDGE_LOOP ( 'NONE', ( #480, #98649, #99477, #52469 ) ) ;
#85767=CARTESIAN_POINT ( 'NONE',  ( 5.994519915287488843, 28.92564299267942118, 4.000000000000000000 ) ) ;
#85768=LINE ( 'NONE', #30709, #50940 ) ;
#85769=CARTESIAN_POINT ( 'NONE',  ( -24.98358986394466186, 3.827854121229849582, 4.315828149752543474 ) ) ;
#85770=CARTESIAN_POINT ( 'NONE',  ( 26.99999999999980105, -22.22500000000000142, 4.412002311789987807 ) ) ;
#85772=ORIENTED_EDGE ( 'NONE', *, *, #87487, .F. ) ;
#85773=EDGE_CURVE ( 'NONE', #122378, #94920, #139045, .T. ) ;
#85774=CARTESIAN_POINT ( 'NONE',  ( -6.121473163371429216, -20.24070752338407431, 7.412974875817805120 ) ) ;
#85777=CARTESIAN_POINT ( 'NONE',  ( 0.000000000000000000, 0.000000000000000000, 5.000000000000000000 ) ) ;
#85778=CARTESIAN_POINT ( 'NONE',  ( 15.18398860626900237, 28.73617430169797871, 5.000000000000000000 ) ) ;
#85779=LINE ( 'NONE', #8190, #105192 ) ;
#85780=FACE_OUTER_BOUND ( 'NONE', #40198, .T. ) ;
#85781=LINE ( 'NONE', #128582, #115194 ) ;
#85783=ADVANCED_FACE ( 'NONE', ( #96213 ), #23679, .F. ) ;
#85784=CARTESIAN_POINT ( 'NONE',  ( 51.29974487139158867, -27.71228299555242103, 4.000000000000000000 ) ) ;
#85785=AXIS2_PLACEMENT_3D ( 'NONE', #46030, #101810, #2467 ) ;
#85786=ORIENTED_EDGE ( 'NONE', *, *, #27161, .T. ) ;
#85789=PLANE ( 'NONE',  #67935 ) ;
#85790=CARTESIAN_POINT ( 'NONE',  ( -33.29974487139158867, -27.71228299555229313, 4.000000000000000000 ) ) ;
#85791=VECTOR ( 'NONE', #42677, 1000.000000000000227 ) ;
#85793=ORIENTED_EDGE ( 'NONE', *, *, #63226, .F. ) ;
#85794=DIRECTION ( 'NONE',  ( 0.7071067811865487940, 0.7071067811865463515, 0.000000000000000000 ) ) ;
#85796=ORIENTED_EDGE ( 'NONE', *, *, #57818, .T. ) ;
#85798=ORIENTED_EDGE ( 'NONE', *, *, #98573, .F. ) ;
#85799=ORIENTED_EDGE ( 'NONE', *, *, #38859, .T. ) ;
#85800=VECTOR ( 'NONE', #56541, 999.9999999999998863 ) ;
#85801=CARTESIAN_POINT ( 'NONE',  ( -26.29298673570676925, -21.74070752338405299, 4.999753212805220670 ) ) ;
#85802=LINE ( 'NONE', #130039, #126426 ) ;
#85803=CARTESIAN_POINT ( 'NONE',  ( 23.84387692260742142, -22.22500000000000142, 4.000000000000000000 ) ) ;
#85804=CARTESIAN_POINT ( 'NONE',  ( 14.51078643762690490, -27.52281430457045275, 5.000000000000000000 ) ) ;
#85805=ORIENTED_EDGE ( 'NONE', *, *, #29731, .F. ) ;
#85806=CARTESIAN_POINT ( 'NONE',  ( -1.499999999999984013, 14.14708470758591119, -0.5283514160166523643 ) ) ;
#85807=DIRECTION ( 'NONE',  ( -0.000000000000000000, -0.3543493200069152693, 0.9351131265310292928 ) ) ;
#85808=ORIENTED_EDGE ( 'NONE', *, *, #19747, .T. ) ;
#85810=DIRECTION ( 'NONE',  ( 0.7071067811865487940, 0.7071067811865463515, 0.000000000000000000 ) ) ;
#85811=DIRECTION ( 'NONE',  ( -0.7071067811865487940, 0.7071067811865463515, 0.000000000000000000 ) ) ;
#85813=AXIS2_PLACEMENT_3D ( 'NONE', #91659, #14809, #125737 ) ;
#85814=CARTESIAN_POINT ( 'NONE',  ( 34.49999999999975842, 19.46425560840029689, 4.994342998332160555 ) ) ;
#85816=ORIENTED_EDGE ( 'NONE', *, *, #31839, .F. ) ;
#85818=DIRECTION ( 'NONE',  ( 0.7071067811865486830, -0.7071067811865464625, -0.000000000000000000 ) ) ;
#85819=EDGE_CURVE ( 'NONE', #60588, #6025, #67949, .T. ) ;
#85820=DIRECTION ( 'NONE',  ( -0.7071067811865486830, 0.7071067811865464625, 0.000000000000000000 ) ) ;
#85821=FACE_OUTER_BOUND ( 'NONE', #37555, .T. ) ;
#85823=ORIENTED_EDGE ( 'NONE', *, *, #72463, .T. ) ;
#85824=DIRECTION ( 'NONE',  ( -0.6830127018922181881, 0.6830127018922202975, -0.2588190451025214056 ) ) ;
#85825=AXIS2_PLACEMENT_3D ( 'NONE', #70451, #134239, #103029 ) ;
#85826=VERTEX_POINT ( 'NONE', #1186 ) ;
#85827=VECTOR ( 'NONE', #35448, 1000.000000000000227 ) ;
#85828=VECTOR ( 'NONE', #50356, 1000.000000000000000 ) ;
#85830=DIRECTION ( 'NONE',  ( -0.000000000000000000, -0.3543493200069152693, 0.9351131265310292928 ) ) ;
#85831=ORIENTED_EDGE ( 'NONE', *, *, #112698, .T. ) ;
#85833=CARTESIAN_POINT ( 'NONE',  ( 28.49999999999981171, 12.05218569542904739, 5.000000000000000000 ) ) ;
#85834=VECTOR ( 'NONE', #61015, 1000.000000000000000 ) ;
#85836=VECTOR ( 'NONE', #8733, 999.9999999999998863 ) ;
#85837=AXIS2_PLACEMENT_3D ( 'NONE', #32979, #77883, #45284 ) ;
#85838=FACE_OUTER_BOUND ( 'NONE', #52254, .T. ) ;
#85839=EDGE_CURVE ( 'NONE', #94607, #3249, #142615, .T. ) ;
#85840=FACE_BOUND ( 'NONE', #40745, .T. ) ;
#85841=LINE ( 'NONE', #42371, #30481 ) ;
#85842=ADVANCED_FACE ( 'NONE', ( #78080 ), #44015, .F. ) ;
#85844=LINE ( 'NONE', #84451, #87324 ) ;
#85846=ORIENTED_EDGE ( 'NONE', *, *, #90672, .F. ) ;
#85847=DIRECTION ( 'NONE',  ( 0.7071067811865487940, 0.7071067811865463515, -0.000000000000000000 ) ) ;
#85849=ORIENTED_EDGE ( 'NONE', *, *, #124152, .T. ) ;
#85853=ADVANCED_FACE ( 'NONE', ( #44771 ), #21543, .T. ) ;
#85854=LINE ( 'NONE', #100317, #18892 ) ;
#85855=VECTOR ( 'NONE', #37458, 1000.000000000000227 ) ;
#85857=DIRECTION ( 'NONE',  ( -0.6830127018922180770, -0.6830127018922204085, -0.2588190451025213501 ) ) ;
#85858=ADVANCED_FACE ( 'NONE', ( #99809 ), #100538, .F. ) ;
#85859=VECTOR ( 'NONE', #50917, 1000.000000000000227 ) ;
#85861=DIRECTION ( 'NONE',  ( -0.3543493200069162685, -0.000000000000000000, -0.9351131265310288487 ) ) ;
#85863=DIRECTION ( 'NONE',  ( 0.6830127018922180770, -0.6830127018922204085, -0.2588190451025213501 ) ) ;
#85864=CARTESIAN_POINT ( 'NONE',  ( 31.17183060077625356, -20.24070752338407431, 4.000000000000000000 ) ) ;
#85865=VECTOR ( 'NONE', #135467, 1000.000000000000000 ) ;
#85866=DIRECTION ( 'NONE',  ( 1.000000000000000000, 0.000000000000000000, 0.000000000000000000 ) ) ;
#85867=PLANE ( 'NONE',  #50886 ) ;
#85868=VERTEX_POINT ( 'NONE', #143312 ) ;
#85869=EDGE_CURVE ( 'NONE', #102338, #111053, #132487, .T. ) ;
#85871=ORIENTED_EDGE ( 'NONE', *, *, #45673, .F. ) ;
#85872=VECTOR ( 'NONE', #97141, 1000.000000000000000 ) ;
#85873=DIRECTION ( 'NONE',  ( 0.3543493200069162685, -0.000000000000000000, -0.9351131265310288487 ) ) ;
#85874=DIRECTION ( 'NONE',  ( 0.7071067811865486830, -0.7071067811865464625, -0.000000000000000000 ) ) ;
#85875=ORIENTED_EDGE ( 'NONE', *, *, #65932, .T. ) ;
#85876=ORIENTED_EDGE ( 'NONE', *, *, #94677, .F. ) ;
#85877=EDGE_LOOP ( 'NONE', ( #58623, #109377, #104870, #98767 ) ) ;
#85879=EDGE_CURVE ( 'NONE', #40957, #114174, #56360, .T. ) ;
#85881=DIRECTION ( 'NONE',  ( -0.3543493200069162685, -0.000000000000000000, -0.9351131265310288487 ) ) ;
#85882=VECTOR ( 'NONE', #86029, 999.9999999999998863 ) ;
#85885=VERTEX_POINT ( 'NONE', #77383 ) ;
#85887=ADVANCED_FACE ( 'NONE', ( #75924 ), #65806, .F. ) ;
#85889=DIRECTION ( 'NONE',  ( -0.7071067811865486830, 0.7071067811865464625, 0.000000000000000000 ) ) ;
#85890=VECTOR ( 'NONE', #12851, 999.9999999999998863 ) ;
#85891=LINE ( 'NONE', #120640, #107703 ) ;
#85892=FACE_OUTER_BOUND ( 'NONE', #131394, .T. ) ;
#85893=EDGE_LOOP ( 'NONE', ( #48433, #131613, #41506, #27969 ) ) ;
#85894=VECTOR ( 'NONE', #111417, 999.9999999999998863 ) ;
#85895=ORIENTED_EDGE ( 'NONE', *, *, #88541, .T. ) ;
#85896=CARTESIAN_POINT ( 'NONE',  ( 0.7071067811865406894, 17.25929247661554200, 5.000000000000000000 ) ) ;
#85897=EDGE_CURVE ( 'NONE', #3922, #103133, #22927, .T. ) ;
#85899=DIRECTION ( 'NONE',  ( 1.000000000000000000, 0.000000000000000000, 0.000000000000000000 ) ) ;
#85901=CARTESIAN_POINT ( 'NONE',  ( -23.84903741288601964, 22.22500000000000142, 0.8029037345187381991 ) ) ;
#85902=ORIENTED_EDGE ( 'NONE', *, *, #72562, .F. ) ;
#85903=ORIENTED_EDGE ( 'NONE', *, *, #77287, .T. ) ;
#85905=LINE ( 'NONE', #119235, #40299 ) ;
#85907=DIRECTION ( 'NONE',  ( -0.7071067811865486830, -0.7071067811865464625, -0.000000000000000000 ) ) ;
#85909=CARTESIAN_POINT ( 'NONE',  ( 17.99999999999987566, 19.93112307739198386, 4.000000000000000000 ) ) ;
#85910=LINE ( 'NONE', #136902, #49218 ) ;
#85911=CARTESIAN_POINT ( 'NONE',  ( 62.99451991528749772, 28.92564299267982264, 4.000000000000000000 ) ) ;
#85912=EDGE_CURVE ( 'NONE', #18830, #21741, #478, .T. ) ;
#85913=DIRECTION ( 'NONE',  ( -0.7071067811865487940, 0.7071067811865463515, -0.000000000000000000 ) ) ;
#85914=ORIENTED_EDGE ( 'NONE', *, *, #18303, .F. ) ;
#85915=EDGE_CURVE ( 'NONE', #92653, #23590, #110650, .T. ) ;
#85916=CARTESIAN_POINT ( 'NONE',  ( 66.29974487139159578, -27.71228299555252406, 4.000000000000000000 ) ) ;
#85917=EDGE_LOOP ( 'NONE', ( #26261, #40882, #87292, #45282 ) ) ;
#85919=CARTESIAN_POINT ( 'NONE',  ( 51.18398860626899705, 28.73617430169823095, 5.000000000000000000 ) ) ;
#85921=ORIENTED_EDGE ( 'NONE', *, *, #143197, .T. ) ;
#85922=DIRECTION ( 'NONE',  ( -0.3543493200069162685, -0.000000000000000000, -0.9351131265310288487 ) ) ;
#85923=EDGE_CURVE ( 'NONE', #61607, #79052, #86808, .T. ) ;
#85924=CARTESIAN_POINT ( 'NONE',  ( 21.29974487139158512, -27.71228299555221142, 4.000000000000000000 ) ) ;
#85925=ORIENTED_EDGE ( 'NONE', *, *, #143075, .T. ) ;
#85928=CARTESIAN_POINT ( 'NONE',  ( -13.71003237941630104, 5.842153316012715258, 5.000000000000000000 ) ) ;
#85929=CARTESIAN_POINT ( 'NONE',  ( 24.18398860626899705, 28.73617430169804265, 5.000000000000000000 ) ) ;
#85930=DIRECTION ( 'NONE',  ( 0.7071067811865487940, 0.7071067811865463515, 0.000000000000000000 ) ) ;
#85931=AXIS2_PLACEMENT_3D ( 'NONE', #22406, #111585, #78992 ) ;
#85932=EDGE_CURVE ( 'NONE', #117254, #57105, #120098, .T. ) ;
#85934=CARTESIAN_POINT ( 'NONE',  ( 19.21321903303347511, 12.75929247661559351, 10.29404684609039755 ) ) ;
#85935=VECTOR ( 'NONE', #94756, 1000.000000000000000 ) ;
#85936=VECTOR ( 'NONE', #83545, 1000.000000000000000 ) ;
#85937=LINE ( 'NONE', #141771, #87756 ) ;
#85938=LINE ( 'NONE', #130901, #53396 ) ;
#85939=DIRECTION ( 'NONE',  ( 0.7071067811865487940, 0.7071067811865463515, 0.000000000000000000 ) ) ;
#85940=ORIENTED_EDGE ( 'NONE', *, *, #94398, .T. ) ;
#85942=ORIENTED_EDGE ( 'NONE', *, *, #9909, .F. ) ;
#85944=AXIS2_PLACEMENT_3D ( 'NONE', #86508, #74196, #132160 ) ;
#85945=VECTOR ( 'NONE', #136728, 1000.000000000000000 ) ;
#85946=CARTESIAN_POINT ( 'NONE',  ( -62.99451991528749772, 28.92564299267982264, 4.000000000000000000 ) ) ;
#85947=VECTOR ( 'NONE', #89743, 1000.000000000000227 ) ;
#85948=CARTESIAN_POINT ( 'NONE',  ( -29.99999999999979039, 20.70535890316558891, 1.956823837851985548 ) ) ;
#85949=ORIENTED_EDGE ( 'NONE', *, *, #62047, .F. ) ;
#85950=VECTOR ( 'NONE', #79353, 1000.000000000000000 ) ;
#85952=CARTESIAN_POINT ( 'NONE',  ( 15.00548008471250228, 28.92564299267927552, 4.000000000000000000 ) ) ;
#85953=EDGE_LOOP ( 'NONE', ( #53710, #49397, #60375, #41301 ) ) ;
#85954=FACE_OUTER_BOUND ( 'NONE', #133369, .T. ) ;
#85955=LINE ( 'NONE', #96782, #34825 ) ;
#85957=VERTEX_POINT ( 'NONE', #109256 ) ;
#85958=ORIENTED_EDGE ( 'NONE', *, *, #55817, .T. ) ;
#85960=CARTESIAN_POINT ( 'NONE',  ( -28.49999999999980460, -17.91344420646044711, 1.358650452708397127 ) ) ;
#85961=VECTOR ( 'NONE', #38744, 1000.000000000000000 ) ;
#85962=CARTESIAN_POINT ( 'NONE',  ( -51.48921356237309510, -27.52281430457091460, 5.000000000000000000 ) ) ;
#85963=EDGE_CURVE ( 'NONE', #98880, #103456, #112822, .T. ) ;
#85965=CARTESIAN_POINT ( 'NONE',  ( 15.70710678118643422, 14.25929247661556687, 5.000000000000000000 ) ) ;
#85966=ADVANCED_FACE ( 'NONE', ( #115641 ), #58511, .F. ) ;
#85968=EDGE_LOOP ( 'NONE', ( #138864, #34943, #75595, #90904 ) ) ;
#85969=VECTOR ( 'NONE', #91735, 1000.000000000000000 ) ;
#85971=CARTESIAN_POINT ( 'NONE',  ( -30.29974487139158867, -27.71228299555227537, 4.000000000000000000 ) ) ;
#85975=DIRECTION ( 'NONE',  ( -0.7071067811865486830, -0.7071067811865464625, -0.000000000000000000 ) ) ;
#85976=EDGE_LOOP ( 'NONE', ( #85463, #42089, #112665, #41142 ) ) ;
#85977=AXIS2_PLACEMENT_3D ( 'NONE', #131838, #133969, #1290 ) ;
#85981=DIRECTION ( 'NONE',  ( -0.000000000000000000, -0.3543493200069152693, 0.9351131265310292928 ) ) ;
#85985=LINE ( 'NONE', #53350, #11727 ) ;
#85986=DIRECTION ( 'NONE',  ( -0.7071067811865486830, -0.7071067811865464625, -0.000000000000000000 ) ) ;
#85987=VECTOR ( 'NONE', #68336, 1000.000000000000000 ) ;
#85988=DIRECTION ( 'NONE',  ( 0.7071067811865486830, -0.7071067811865464625, -0.000000000000000000 ) ) ;
#85990=VERTEX_POINT ( 'NONE', #25086 ) ;
#85992=DIRECTION ( 'NONE',  ( -0.7071067811865487940, 0.7071067811865463515, 0.000000000000000000 ) ) ;
#85996=ORIENTED_EDGE ( 'NONE', *, *, #55572, .T. ) ;
#85999=ORIENTED_EDGE ( 'NONE', *, *, #245, .T. ) ;
#86001=CARTESIAN_POINT ( 'NONE',  ( -34.92500000000001137, 17.81665438641024579, 4.500000000000000888 ) ) ;
#86002=EDGE_CURVE ( 'NONE', #540, #133266, #91105, .T. ) ;
#86003=VECTOR ( 'NONE', #34843, 1000.000000000000000 ) ;
#86005=CARTESIAN_POINT ( 'NONE',  ( 27.18398860626900060, 28.73617430169806042, 5.000000000000000000 ) ) ;
#86006=EDGE_LOOP ( 'NONE', ( #89741, #119831, #53384, #126137 ) ) ;
#86007=CIRCLE ( 'NONE', #35020, 5.968999999999998529 ) ;
#86009=DIRECTION ( 'NONE',  ( -0.7071067811865487940, 0.7071067811865463515, 0.000000000000000000 ) ) ;
#86011=CARTESIAN_POINT ( 'NONE',  ( 34.92499999999998295, -9.183345613589446899, 4.500000000000000888 ) ) ;
#86012=DIRECTION ( 'NONE',  ( -0.7071067811865486830, -0.7071067811865464625, 0.000000000000000000 ) ) ;
#86014=VECTOR ( 'NONE', #65276, 1000.000000000000227 ) ;
#86015=( BOUNDED_CURVE ( )  B_SPLINE_CURVE ( 3, ( #40007, #94344, #61067, #39273 ),
 .UNSPECIFIED., .F., .T. ) 
 B_SPLINE_CURVE_WITH_KNOTS ( ( 4, 4 ),
 ( 5.143245962375964986, 6.645403452391247079 ),
 .UNSPECIFIED. ) 
 CURVE ( )  GEOMETRIC_REPRESENTATION_ITEM ( )  RATIONAL_B_SPLINE_CURVE ( ( 1.000000000000000000, 0.8206354192515239454, 0.8206354192515239454, 1.000000000000000000 ) ) 
 REPRESENTATION_ITEM ( '' )  );
#86017=ORIENTED_EDGE ( 'NONE', *, *, #121146, .T. ) ;
#86019=ADVANCED_FACE ( 'NONE', ( #135324 ), #36008, .F. ) ;
#86020=EDGE_CURVE ( 'NONE', #91527, #139662, #26538, .T. ) ;
#86021=CARTESIAN_POINT ( 'NONE',  ( -26.99999999999981526, -0.2811185226894545863, -5.995736974527452467 ) ) ;
#86022=LINE ( 'NONE', #55550, #43314 ) ;
#86023=CARTESIAN_POINT ( 'NONE',  ( -18.29974487139159223, -27.71228299555219010, 4.000000000000000000 ) ) ;
#86024=LINE ( 'NONE', #10574, #101476 ) ;
#86026=FACE_OUTER_BOUND ( 'NONE', #142358, .T. ) ;
#86027=EDGE_CURVE ( 'NONE', #106514, #114480, #49024, .T. ) ;
#86028=EDGE_CURVE ( 'NONE', #13154, #49277, #136006, .T. ) ;
#86029=DIRECTION ( 'NONE',  ( 0.7071067811865487940, 0.7071067811865463515, 0.000000000000000000 ) ) ;
#86030=ORIENTED_EDGE ( 'NONE', *, *, #140576, .F. ) ;
#86031=VERTEX_POINT ( 'NONE', #92482 ) ;
#86032=ORIENTED_EDGE ( 'NONE', *, *, #111123, .T. ) ;
#86033=EDGE_CURVE ( 'NONE', #15696, #54913, #93216, .T. ) ;
#86034=ORIENTED_EDGE ( 'NONE', *, *, #62050, .F. ) ;
#86036=VECTOR ( 'NONE', #88972, 999.9999999999998863 ) ;
#86037=LINE ( 'NONE', #20767, #131173 ) ;
#86038=VECTOR ( 'NONE', #120622, 1000.000000000000000 ) ;
#86039=EDGE_CURVE ( 'NONE', #62749, #121709, #113526, .T. ) ;
#86040=AXIS2_PLACEMENT_3D ( 'NONE', #80171, #3274, #78722 ) ;
#86041=CARTESIAN_POINT ( 'NONE',  ( -34.49999999999975131, -2.568876922607788327, 4.000000000000000000 ) ) ;
#86042=ORIENTED_EDGE ( 'NONE', *, *, #71000, .F. ) ;
#86047=VECTOR ( 'NONE', #30869, 1000.000000000000227 ) ;
#86048=AXIS2_PLACEMENT_3D ( 'NONE', #141980, #42668, #75985 ) ;
#86049=VECTOR ( 'NONE', #124630, 1000.000000000000000 ) ;
#86052=FACE_OUTER_BOUND ( 'NONE', #29012, .T. ) ;
#86053=ORIENTED_EDGE ( 'NONE', *, *, #40754, .T. ) ;
#86055=LINE ( 'NONE', #52691, #5515 ) ;
#86058=PLANE ( 'NONE',  #122259 ) ;
#86059=VERTEX_POINT ( 'NONE', #114254 ) ;
#86060=VERTEX_POINT ( 'NONE', #59205 ) ;
#86061=ORIENTED_EDGE ( 'NONE', *, *, #82077, .T. ) ;
#86062=VECTOR ( 'NONE', #116844, 1000.000000000000000 ) ;
#86064=ADVANCED_FACE ( 'NONE', ( #14929 ), #39576, .T. ) ;
#86065=ORIENTED_EDGE ( 'NONE', *, *, #54658, .T. ) ;
#86066=ORIENTED_EDGE ( 'NONE', *, *, #124592, .F. ) ;
#86067=DIRECTION ( 'NONE',  ( 0.7071067811865487940, 0.7071067811865463515, 0.000000000000000000 ) ) ;
#86070=DIRECTION ( 'NONE',  ( 0.7071067811865487940, 0.7071067811865463515, 0.000000000000000000 ) ) ;
#86071=LINE ( 'NONE', #30994, #111459 ) ;
#86073=VERTEX_POINT ( 'NONE', #41696 ) ;
#86074=CARTESIAN_POINT ( 'NONE',  ( -9.183988606268997046, 28.73617430169793607, 5.000000000000000000 ) ) ;
#86075=DIRECTION ( 'NONE',  ( -0.000000000000000000, 0.000000000000000000, 1.000000000000000000 ) ) ;
#86076=LINE ( 'NONE', #87503, #72223 ) ;
#86077=VECTOR ( 'NONE', #88202, 1000.000000000000000 ) ;
#86078=FACE_OUTER_BOUND ( 'NONE', #1139, .T. ) ;
#86079=EDGE_CURVE ( 'NONE', #1659, #54031, #6878, .T. ) ;
#86080=ORIENTED_EDGE ( 'NONE', *, *, #24417, .F. ) ;
#86082=PLANE ( 'NONE',  #120070 ) ;
#86084=EDGE_CURVE ( 'NONE', #39673, #80757, #7614, .T. ) ;
#86086=ORIENTED_EDGE ( 'NONE', *, *, #40865, .T. ) ;
#86087=VERTEX_POINT ( 'NONE', #40985 ) ;
#86089=ORIENTED_EDGE ( 'NONE', *, *, #90452, .F. ) ;
#86091=CARTESIAN_POINT ( 'NONE',  ( -3.792893218813424117, 12.75929247661558996, 5.000000000000000000 ) ) ;
#86092=CARTESIAN_POINT ( 'NONE',  ( -26.99451991528749417, 28.92564299267956685, 4.000000000000000000 ) ) ;
#86093=ORIENTED_EDGE ( 'NONE', *, *, #105807, .T. ) ;
#86099=DIRECTION ( 'NONE',  ( -0.000000000000000000, 0.3543493200069153248, 0.9351131265310292928 ) ) ;
#86100=ADVANCED_FACE ( 'NONE', ( #30843 ), #85180, .T. ) ;
#86102=VERTEX_POINT ( 'NONE', #129404 ) ;
#86103=ORIENTED_EDGE ( 'NONE', *, *, #46468, .T. ) ;
#86105=EDGE_LOOP ( 'NONE', ( #107373, #60852, #57483, #23772 ) ) ;
#86106=DIRECTION ( 'NONE',  ( 0.7071067811865487940, 0.7071067811865463515, 0.000000000000000000 ) ) ;
#86107=PLANE ( 'NONE',  #95036 ) ;
#86108=VECTOR ( 'NONE', #140159, 999.9999999999998863 ) ;
#86109=CARTESIAN_POINT ( 'NONE',  ( -5.994519915287488843, 28.92564299267942118, 4.000000000000000000 ) ) ;
#86110=EDGE_CURVE ( 'NONE', #101632, #42277, #60641, .T. ) ;
#86111=DIRECTION ( 'NONE',  ( 0.7071067811865487940, 0.7071067811865463515, 0.000000000000000000 ) ) ;
#86112=CARTESIAN_POINT ( 'NONE',  ( -2.207106781186518596, -2.240707523384260824, 5.000000000000000000 ) ) ;
#86116=LINE ( 'NONE', #29571, #95202 ) ;
#86118=DIRECTION ( 'NONE',  ( -0.3543493200069162685, -0.000000000000000000, -0.9351131265310288487 ) ) ;
#86120=DIRECTION ( 'NONE',  ( -0.7071067811865486830, -0.7071067811865464625, 0.000000000000000000 ) ) ;
#86121=ORIENTED_EDGE ( 'NONE', *, *, #142315, .F. ) ;
#86122=DIRECTION ( 'NONE',  ( 0.6830127018922181881, 0.6830127018922202975, -0.2588190451025214056 ) ) ;
#86123=CARTESIAN_POINT ( 'NONE',  ( 25.17183060077630330, 15.75929247661556332, 4.000000000000000000 ) ) ;
#86124=ORIENTED_EDGE ( 'NONE', *, *, #99471, .T. ) ;
#86125=EDGE_CURVE ( 'NONE', #71270, #65995, #83810, .T. ) ;
#86126=LINE ( 'NONE', #131057, #80798 ) ;
#86128=EDGE_LOOP ( 'NONE', ( #140268, #83401, #83293, #67506 ) ) ;
#86129=CARTESIAN_POINT ( 'NONE',  ( 9.328169399223463998, -12.74070752338415247, 4.000000000000000000 ) ) ;
#86130=VECTOR ( 'NONE', #54426, 1000.000000000000000 ) ;
#86131=ORIENTED_EDGE ( 'NONE', *, *, #48328, .T. ) ;
#86132=LINE ( 'NONE', #64375, #76769 ) ;
#86133=VERTEX_POINT ( 'NONE', #5467 ) ;
#86135=EDGE_CURVE ( 'NONE', #7775, #53800, #72943, .T. ) ;
#86137=CARTESIAN_POINT ( 'NONE',  ( -34.92500000000001137, 7.701930566820932356, 4.500000000000000888 ) ) ;
#86138=DIRECTION ( 'NONE',  ( -0.7071067811865487940, 0.7071067811865463515, -0.000000000000000000 ) ) ;
#86139=CARTESIAN_POINT ( 'NONE',  ( 20.25795612380215971, -2.670494247963030698, 4.000000000000000000 ) ) ;
#86140=CARTESIAN_POINT ( 'NONE',  ( 8.999999999999941380, -6.033600742197681832, 5.000000000000000000 ) ) ;
#86144=VECTOR ( 'NONE', #33016, 1000.000000000000000 ) ;
#86145=VECTOR ( 'NONE', #24035, 1000.000000000000000 ) ;
#86146=VECTOR ( 'NONE', #113099, 1000.000000000000227 ) ;
#86147=CARTESIAN_POINT ( 'NONE',  ( -25.82816939922334853, 15.75929247661557042, 4.000000000000000000 ) ) ;
#86148=DIRECTION ( 'NONE',  ( -0.7071067811865486830, -0.7071067811865464625, 0.000000000000000000 ) ) ;
#86149=VERTEX_POINT ( 'NONE', #85909 ) ;
#86150=ORIENTED_EDGE ( 'NONE', *, *, #19505, .T. ) ;
#86153=EDGE_CURVE ( 'NONE', #18419, #97224, #84506, .T. ) ;
#86154=CARTESIAN_POINT ( 'NONE',  ( 0.000000000000000000, -21.72500000000000142, 4.500000000000000888 ) ) ;
#86155=ORIENTED_EDGE ( 'NONE', *, *, #16713, .F. ) ;
#86158=DIRECTION ( 'NONE',  ( -0.6830127018922181881, 0.6830127018922202975, -0.2588190451025214056 ) ) ;
#86159=VECTOR ( 'NONE', #48183, 1000.000000000000000 ) ;
#86162=ORIENTED_EDGE ( 'NONE', *, *, #143533, .F. ) ;
#86163=CARTESIAN_POINT ( 'NONE',  ( 3.707013264293012256, -21.74070752338405654, 4.999753212805217117 ) ) ;
#86165=EDGE_CURVE ( 'NONE', #127309, #63645, #62045, .T. ) ;
#86167=LINE ( 'NONE', #53536, #12760 ) ;
#86168=EDGE_LOOP ( 'NONE', ( #103272, #37591, #131533 ) ) ;
#86169=CARTESIAN_POINT ( 'NONE',  ( 0.000000000000000000, 21.72500000000000142, 4.500000000000000888 ) ) ;
#86171=CARTESIAN_POINT ( 'NONE',  ( -5.700255128608413102, -27.71228299555201957, 4.000000000000000000 ) ) ;
#86172=DIRECTION ( 'NONE',  ( 1.000000000000000000, 0.000000000000000000, 0.000000000000000000 ) ) ;
#86174=ORIENTED_EDGE ( 'NONE', *, *, #60650, .T. ) ;
#86175=ORIENTED_EDGE ( 'NONE', *, *, #131799, .F. ) ;
#86178=VERTEX_POINT ( 'NONE', #139618 ) ;
#86180=DIRECTION ( 'NONE',  ( -0.6830127018922180770, -0.6830127018922204085, -0.2588190451025213501 ) ) ;
#86181=VERTEX_POINT ( 'NONE', #106203 ) ;
#86182=LINE ( 'NONE', #74607, #35221 ) ;
#86183=CARTESIAN_POINT ( 'NONE',  ( 14.81601139373099585, 28.73617430169776910, 5.000000000000000000 ) ) ;
#86184=AXIS2_PLACEMENT_3D ( 'NONE', #117214, #138291, #38970 ) ;
#86186=VERTEX_POINT ( 'NONE', #116403 ) ;
#86187=VECTOR ( 'NONE', #130492, 1000.000000000000000 ) ;
#86188=DIRECTION ( 'NONE',  ( -0.7071067811865487940, 0.7071067811865463515, -0.000000000000000000 ) ) ;
#86189=EDGE_CURVE ( 'NONE', #50892, #94083, #17092, .T. ) ;
#86190=DIRECTION ( 'NONE',  ( -0.7071067811865486830, -0.7071067811865464625, -0.000000000000000000 ) ) ;
#86192=VECTOR ( 'NONE', #731, 999.9999999999998863 ) ;
#86194=EDGE_CURVE ( 'NONE', #73530, #135631, #73616, .T. ) ;
#86195=ORIENTED_EDGE ( 'NONE', *, *, #52871, .F. ) ;
#86196=ORIENTED_EDGE ( 'NONE', *, *, #117004, .T. ) ;
#86197=EDGE_LOOP ( 'NONE', ( #74647, #125854, #88388 ) ) ;
#86198=CARTESIAN_POINT ( 'NONE',  ( 0.000000000000000000, 0.000000000000000000, 5.000000000000000000 ) ) ;
#86199=ADVANCED_FACE ( 'NONE', ( #51877 ), #140295, .F. ) ;
#86200=EDGE_CURVE ( 'NONE', #128517, #71727, #52561, .T. ) ;
#86201=CARTESIAN_POINT ( 'NONE',  ( 36.18398860626899705, 28.73617430169812437, 5.000000000000000000 ) ) ;
#86203=VECTOR ( 'NONE', #100149, 999.9999999999998863 ) ;
#86204=PLANE ( 'NONE',  #34135 ) ;
#86205=FACE_OUTER_BOUND ( 'NONE', #84378, .T. ) ;
#86206=EDGE_CURVE ( 'NONE', #128869, #103370, #56190, .T. ) ;
#86210=VERTEX_POINT ( 'NONE', #33002 ) ;
#86211=ORIENTED_EDGE ( 'NONE', *, *, #7550, .T. ) ;
#86212=DIRECTION ( 'NONE',  ( -0.000000000000000000, -0.3543493200069152693, 0.9351131265310292928 ) ) ;
#86214=ORIENTED_EDGE ( 'NONE', *, *, #24513, .F. ) ;
#86215=VERTEX_POINT ( 'NONE', #120658 ) ;
#86216=VECTOR ( 'NONE', #54135, 1000.000000000000000 ) ;
#86217=VECTOR ( 'NONE', #79036, 1000.000000000000227 ) ;
#86218=EDGE_CURVE ( 'NONE', #5541, #69693, #31540, .T. ) ;
#86219=EDGE_CURVE ( 'NONE', #66330, #76165, #21376, .T. ) ;
#86221=EDGE_LOOP ( 'NONE', ( #6759, #6693, #98857, #39098 ) ) ;
#86224=CARTESIAN_POINT ( 'NONE',  ( 8.816011393731004731, 28.73617430169781173, 5.000000000000000000 ) ) ;
#86229=LINE ( 'NONE', #130453, #7294 ) ;
#86233=ORIENTED_EDGE ( 'NONE', *, *, #54657, .T. ) ;
#86239=DIRECTION ( 'NONE',  ( -0.000000000000000000, -0.3543493200069152693, 0.9351131265310292928 ) ) ;
#86241=ORIENTED_EDGE ( 'NONE', *, *, #33444, .T. ) ;
#86242=VECTOR ( 'NONE', #5882, 1000.000000000000000 ) ;
#86243=EDGE_CURVE ( 'NONE', #68263, #56149, #33699, .T. ) ;
#86244=EDGE_LOOP ( 'NONE', ( #142021, #47920, #73107, #33352 ) ) ;
#86246=LINE ( 'NONE', #55049, #101617 ) ;
#86248=PLANE ( 'NONE',  #68272 ) ;
#86249=DIRECTION ( 'NONE',  ( 0.7071067811865487940, 0.7071067811865463515, 0.000000000000000000 ) ) ;
#86250=CARTESIAN_POINT ( 'NONE',  ( 72.48921356237309510, -27.52281430457106026, 5.000000000000000000 ) ) ;
#86252=AXIS2_PLACEMENT_3D ( 'NONE', #42780, #65975, #10810 ) ;
#86253=VECTOR ( 'NONE', #21998, 1000.000000000000000 ) ;
#86254=CARTESIAN_POINT ( 'NONE',  ( -22.78678096696627264, 12.75929247661559351, 10.29404684609029985 ) ) ;
#86256=PLANE ( 'NONE',  #57563 ) ;
#86257=EDGE_CURVE ( 'NONE', #101316, #58036, #141744, .T. ) ;
#86258=DIRECTION ( 'NONE',  ( -0.7071067811865486830, 0.7071067811865464625, 0.000000000000000000 ) ) ;
#86260=VERTEX_POINT ( 'NONE', #130873 ) ;
#86261=ADVANCED_FACE ( 'NONE', ( #98228 ), #43845, .F. ) ;
#86262=ORIENTED_EDGE ( 'NONE', *, *, #12186, .T. ) ;
#86264=VERTEX_POINT ( 'NONE', #122093 ) ;
#86266=ORIENTED_EDGE ( 'NONE', *, *, #90707, .F. ) ;
#86268=VERTEX_POINT ( 'NONE', #111211 ) ;
#86270=ORIENTED_EDGE ( 'NONE', *, *, #74756, .T. ) ;
#86271=CARTESIAN_POINT ( 'NONE',  ( 57.29974487139158157, -27.71228299555246011, 4.000000000000000000 ) ) ;
#86272=LINE ( 'NONE', #73954, #140434 ) ;
#86273=DIRECTION ( 'NONE',  ( -0.7071067811865487940, 0.7071067811865463515, 0.000000000000000000 ) ) ;
#86276=ORIENTED_EDGE ( 'NONE', *, *, #13405, .F. ) ;
#86277=FACE_OUTER_BOUND ( 'NONE', #40684, .T. ) ;
#86278=FACE_OUTER_BOUND ( 'NONE', #79877, .T. ) ;
#86281=ORIENTED_EDGE ( 'NONE', *, *, #71649, .F. ) ;
#86284=DIRECTION ( 'NONE',  ( -0.6830127018922181881, 0.6830127018922202975, -0.2588190451025214056 ) ) ;
#86285=EDGE_CURVE ( 'NONE', #62294, #90422, #34392, .T. ) ;
#86286=DIRECTION ( 'NONE',  ( -0.7071067811865487940, 0.7071067811865463515, 0.000000000000000000 ) ) ;
#86287=VERTEX_POINT ( 'NONE', #134433 ) ;
#86289=DIRECTION ( 'NONE',  ( 0.7071067811865487940, 0.7071067811865463515, 0.000000000000000000 ) ) ;
#86290=ORIENTED_EDGE ( 'NONE', *, *, #27747, .T. ) ;
#86291=CARTESIAN_POINT ( 'NONE',  ( -9.437085545171145284, -22.22500000000000142, -4.658323575210101986 ) ) ;
#86292=LINE ( 'NONE', #63127, #7018 ) ;
#86293=CARTESIAN_POINT ( 'NONE',  ( 2.865004262483764830, 3.759292476615685441, 15.36553568819725513 ) ) ;
#86294=LINE ( 'NONE', #75413, #63444 ) ;
#86295=ORIENTED_EDGE ( 'NONE', *, *, #76425, .T. ) ;
#86296=AXIS2_PLACEMENT_3D ( 'NONE', #85150, #129365, #30052 ) ;
#86298=ADVANCED_FACE ( 'NONE', ( #135847 ), #103202, .F. ) ;
#86300=CARTESIAN_POINT ( 'NONE',  ( -10.17183060077640455, -2.240707523384259492, 4.000000000000000000 ) ) ;
#86301=CARTESIAN_POINT ( 'NONE',  ( 10.49999999999992717, 3.431123077392147724, 4.000000000000000000 ) ) ;
#86302=EDGE_LOOP ( 'NONE', ( #141675, #57199, #7700, #126172 ) ) ;
#86303=CARTESIAN_POINT ( 'NONE',  ( -34.92500000000001137, -22.22500000000000142, 4.500000000000000888 ) ) ;
#86305=FACE_OUTER_BOUND ( 'NONE', #99084, .T. ) ;
#86308=ORIENTED_EDGE ( 'NONE', *, *, #37997, .F. ) ;
#86309=EDGE_CURVE ( 'NONE', #19139, #24144, #24235, .T. ) ;
#86311=DIRECTION ( 'NONE',  ( -0.000000000000000000, 0.3543493200069153248, 0.9351131265310292928 ) ) ;
#86313=VERTEX_POINT ( 'NONE', #3171 ) ;
#86314=CARTESIAN_POINT ( 'NONE',  ( 19.82816939922339117, -20.24070752338407431, 4.000000000000000000 ) ) ;
#86316=EDGE_CURVE ( 'NONE', #108968, #93841, #1711, .T. ) ;
#86317=LINE ( 'NONE', #107329, #115513 ) ;
#86318=LINE ( 'NONE', #32650, #60145 ) ;
#86319=CARTESIAN_POINT ( 'NONE',  ( 16.17183060077636370, 18.75929247661553134, 4.000000000000000000 ) ) ;
#86320=DIRECTION ( 'NONE',  ( -0.000000000000000000, -0.3543493200069152693, 0.9351131265310292928 ) ) ;
#86321=VECTOR ( 'NONE', #72708, 1000.000000000000000 ) ;
#86322=LINE ( 'NONE', #130542, #37952 ) ;
#86323=CARTESIAN_POINT ( 'NONE',  ( 63.18398860626900415, 28.73617430169831621, 5.000000000000000000 ) ) ;
#86324=CARTESIAN_POINT ( 'NONE',  ( 7.171830600776425868, -8.240707523384203981, 4.000000000000000000 ) ) ;
#86325=CARTESIAN_POINT ( 'NONE',  ( -62.99451991528749772, 28.92564299267982264, 4.000000000000000000 ) ) ;
#86327=LINE ( 'NONE', #130546, #11234 ) ;
#86328=FACE_OUTER_BOUND ( 'NONE', #24474, .T. ) ;
#86329=EDGE_LOOP ( 'NONE', ( #128936, #107934, #56152, #117525 ) ) ;
#86330=ADVANCED_FACE ( 'NONE', ( #80768 ), #135163, .F. ) ;
#86331=ORIENTED_EDGE ( 'NONE', *, *, #134343, .T. ) ;
#86332=ORIENTED_EDGE ( 'NONE', *, *, #87918, .F. ) ;
#86334=EDGE_CURVE ( 'NONE', #18953, #52975, #70632, .T. ) ;
#86335=ORIENTED_EDGE ( 'NONE', *, *, #48223, .T. ) ;
#86336=ORIENTED_EDGE ( 'NONE', *, *, #103996, .T. ) ;
#86337=ORIENTED_EDGE ( 'NONE', *, *, #45673, .T. ) ;
#86338=PLANE ( 'NONE',  #59470 ) ;
#86339=CARTESIAN_POINT ( 'NONE',  ( 19.49999999999986500, -4.912538124160707120, 4.000000000000000000 ) ) ;
#86340=VECTOR ( 'NONE', #47724, 1000.000000000000000 ) ;
#86341=ORIENTED_EDGE ( 'NONE', *, *, #137198, .F. ) ;
#86343=DIRECTION ( 'NONE',  ( 0.7071067811865487940, 0.7071067811865463515, 0.000000000000000000 ) ) ;
#86344=DIRECTION ( 'NONE',  ( 1.000000000000000000, -0.000000000000000000, 0.000000000000000000 ) ) ;
#86345=PLANE ( 'NONE',  #32752 ) ;
#86347=ORIENTED_EDGE ( 'NONE', *, *, #93318, .F. ) ;
#86348=ADVANCED_FACE ( 'NONE', ( #112660 ), #124958, .F. ) ;
#86350=FACE_OUTER_BOUND ( 'NONE', #135228, .T. ) ;
#86351=AXIS2_PLACEMENT_3D ( 'NONE', #60892, #128947, #118035 ) ;
#86352=PLANE ( 'NONE',  #67888 ) ;
#86353=CARTESIAN_POINT ( 'NONE',  ( 17.20710678118643244, 18.75929247661552068, 5.000000000000000000 ) ) ;
#86354=DIRECTION ( 'NONE',  ( 0.6830127018922180770, -0.6830127018922204085, -0.2588190451025213501 ) ) ;
#86355=LINE ( 'NONE', #8719, #98597 ) ;
#86356=DIRECTION ( 'NONE',  ( -0.7071067811865487940, 0.7071067811865463515, -0.000000000000000000 ) ) ;
#86357=CARTESIAN_POINT ( 'NONE',  ( 0.000000000000000000, 0.000000000000000000, 5.000000000000000000 ) ) ;
#86358=ORIENTED_EDGE ( 'NONE', *, *, #56704, .F. ) ;
#86359=ORIENTED_EDGE ( 'NONE', *, *, #122350, .F. ) ;
#86361=EDGE_LOOP ( 'NONE', ( #81320, #34341, #934, #15940 ) ) ;
#86362=LINE ( 'NONE', #42151, #96913 ) ;
#86363=DIRECTION ( 'NONE',  ( -0.7071067811865487940, 0.7071067811865463515, -0.000000000000000000 ) ) ;
#86364=VECTOR ( 'NONE', #95730, 1000.000000000000000 ) ;
#86365=CARTESIAN_POINT ( 'NONE',  ( 27.32816939922334143, -0.7407075233842683737, 4.000000000000000000 ) ) ;
#86366=LINE ( 'NONE', #8049, #123321 ) ;
#86367=VECTOR ( 'NONE', #38498, 1000.000000000000000 ) ;
#86368=LINE ( 'NONE', #85615, #11881 ) ;
#86369=CARTESIAN_POINT ( 'NONE',  ( -10.11017322888203651, -22.22500000000000497, 4.785647885939354751 ) ) ;
#86370=VECTOR ( 'NONE', #64129, 1000.000000000000000 ) ;
#86372=EDGE_LOOP ( 'NONE', ( #127756, #52509, #134821, #22955 ) ) ;
#86373=FACE_OUTER_BOUND ( 'NONE', #15444, .T. ) ;
#86374=ORIENTED_EDGE ( 'NONE', *, *, #128292, .T. ) ;
#86375=VECTOR ( 'NONE', #62217, 1000.000000000000000 ) ;
#86376=VECTOR ( 'NONE', #7316, 1000.000000000000227 ) ;
#86378=FACE_OUTER_BOUND ( 'NONE', #41579, .T. ) ;
#86379=LINE ( 'NONE', #109537, #57035 ) ;
#86380=CARTESIAN_POINT ( 'NONE',  ( 0.000000000000000000, 0.000000000000000000, 5.000000000000000000 ) ) ;
#86381=ORIENTED_EDGE ( 'NONE', *, *, #101785, .F. ) ;
#86383=ORIENTED_EDGE ( 'NONE', *, *, #112748, .T. ) ;
#86384=DIRECTION ( 'NONE',  ( 0.7071067811865486830, -0.7071067811865464625, -0.000000000000000000 ) ) ;
#86385=DIRECTION ( 'NONE',  ( -1.000000000000000000, 0.000000000000000000, 0.000000000000000000 ) ) ;
#86387=EDGE_CURVE ( 'NONE', #23874, #116753, #114091, .T. ) ;
#86390=EDGE_CURVE ( 'NONE', #101224, #79010, #57596, .T. ) ;
#86391=ORIENTED_EDGE ( 'NONE', *, *, #68503, .T. ) ;
#86394=ORIENTED_EDGE ( 'NONE', *, *, #114991, .F. ) ;
#86395=ORIENTED_EDGE ( 'NONE', *, *, #11552, .F. ) ;
#86396=ORIENTED_EDGE ( 'NONE', *, *, #68805, .F. ) ;
#86398=AXIS2_PLACEMENT_3D ( 'NONE', #109953, #132473, #86798 ) ;
#86401=ORIENTED_EDGE ( 'NONE', *, *, #6116, .F. ) ;
#86402=VECTOR ( 'NONE', #125701, 1000.000000000000000 ) ;
#86403=CARTESIAN_POINT ( 'NONE',  ( -9.183988606268997046, 28.73617430169793607, 5.000000000000000000 ) ) ;
#86404=EDGE_CURVE ( 'NONE', #108193, #6023, #69175, .T. ) ;
#86405=CARTESIAN_POINT ( 'NONE',  ( -17.67183060077635304, -9.740707523384180888, 4.000000000000000000 ) ) ;
#86406=DIRECTION ( 'NONE',  ( -0.7071067811865486830, -0.7071067811865464625, 0.000000000000000000 ) ) ;
#86407=EDGE_CURVE ( 'NONE', #116521, #26660, #122827, .T. ) ;
#86408=FACE_BOUND ( 'NONE', #6365, .T. ) ;
#86409=ORIENTED_EDGE ( 'NONE', *, *, #36977, .F. ) ;
#86410=EDGE_CURVE ( 'NONE', #23670, #65156, #3849, .T. ) ;
#86411=DIRECTION ( 'NONE',  ( 0.7071067811865487940, -0.7071067811865463515, 0.000000000000000000 ) ) ;
#86413=VERTEX_POINT ( 'NONE', #92314 ) ;
#86414=DIRECTION ( 'NONE',  ( -0.7071067811865486830, 0.7071067811865464625, 0.000000000000000000 ) ) ;
#86415=ORIENTED_EDGE ( 'NONE', *, *, #62804, .T. ) ;
#86417=CARTESIAN_POINT ( 'NONE',  ( -34.92500000000001137, -22.22500000000000142, 4.000000000000000000 ) ) ;
#86418=EDGE_CURVE ( 'NONE', #41631, #61971, #81496, .T. ) ;
#86419=ORIENTED_EDGE ( 'NONE', *, *, #111637, .T. ) ;
#86420=AXIS2_PLACEMENT_3D ( 'NONE', #32643, #112336, #131958 ) ;
#86423=ORIENTED_EDGE ( 'NONE', *, *, #62976, .F. ) ;
#86424=CARTESIAN_POINT ( 'NONE',  ( -25.82816939922335209, -17.24070752338409918, 4.000000000000000000 ) ) ;
#86425=LINE ( 'NONE', #11659, #3229 ) ;
#86426=EDGE_LOOP ( 'NONE', ( #19288, #4943, #83, #110914 ) ) ;
#86427=DIRECTION ( 'NONE',  ( 0.6830127018922180770, -0.6830127018922204085, -0.2588190451025213501 ) ) ;
#86429=VECTOR ( 'NONE', #40873, 1000.000000000000000 ) ;
#86430=( BOUNDED_CURVE ( )  B_SPLINE_CURVE ( 3, ( #99724, #24317, #79465, #122919 ),
 .UNSPECIFIED., .F., .F. ) 
 B_SPLINE_CURVE_WITH_KNOTS ( ( 4, 4 ),
 ( 1.864375635226932282, 1.933014472006575613 ),
 .UNSPECIFIED. ) 
 CURVE ( )  GEOMETRIC_REPRESENTATION_ITEM ( )  RATIONAL_B_SPLINE_CURVE ( ( 1.000000000000000000, 0.9996074310407760954, 0.9996074310407760954, 1.000000000000000000 ) ) 
 REPRESENTATION_ITEM ( '' )  );
#86431=CARTESIAN_POINT ( 'NONE',  ( -0.1839886062690032631, 28.73617430169787568, 5.000000000000000000 ) ) ;
#86433=DIRECTION ( 'NONE',  ( -0.3543493200069162685, -0.000000000000000000, -0.9351131265310288487 ) ) ;
#86434=LINE ( 'NONE', #19719, #9320 ) ;
#86436=EDGE_CURVE ( 'NONE', #119557, #50386, #37247, .T. ) ;
#86437=VECTOR ( 'NONE', #59585, 1000.000000000000000 ) ;
#86438=VERTEX_POINT ( 'NONE', #103896 ) ;
#86440=DIRECTION ( 'NONE',  ( 0.7071067811865487940, -0.7071067811865463515, 0.000000000000000000 ) ) ;
#86441=ORIENTED_EDGE ( 'NONE', *, *, #75603, .F. ) ;
#86442=ORIENTED_EDGE ( 'NONE', *, *, #36590, .T. ) ;
#86443=VERTEX_POINT ( 'NONE', #4543 ) ;
#86444=CARTESIAN_POINT ( 'NONE',  ( 4.998069433178977228, -22.22500000000000142, 4.500000000000000888 ) ) ;
#86445=PLANE ( 'NONE',  #10841 ) ;
#86446=LINE ( 'NONE', #85694, #74058 ) ;
#86447=AXIS2_PLACEMENT_3D ( 'NONE', #55521, #143228, #107728 ) ;
#86448=ORIENTED_EDGE ( 'NONE', *, *, #86501, .T. ) ;
#86450=EDGE_CURVE ( 'NONE', #120495, #135320, #48852, .T. ) ;
#86453=CARTESIAN_POINT ( 'NONE',  ( 2.999999999999975131, 7.007997736742450634, -8.085015511992105885 ) ) ;
#86454=VERTEX_POINT ( 'NONE', #67780 ) ;
#86456=FACE_OUTER_BOUND ( 'NONE', #113049, .T. ) ;
#86458=LINE ( 'NONE', #95881, #139911 ) ;
#86460=DIRECTION ( 'NONE',  ( 0.7071067811865487940, 0.7071067811865463515, -0.000000000000000000 ) ) ;
#86461=ORIENTED_EDGE ( 'NONE', *, *, #82591, .T. ) ;
#86463=ORIENTED_EDGE ( 'NONE', *, *, #96361, .T. ) ;
#86464=CARTESIAN_POINT ( 'NONE',  ( -22.49999999999984368, -1.695981523266240076, 4.571483868317929300 ) ) ;
#86465=CARTESIAN_POINT ( 'NONE',  ( -21.18398860626899349, 28.73617430169802134, 5.000000000000000000 ) ) ;
#86466=LINE ( 'NONE', #97280, #86605 ) ;
#86467=ORIENTED_EDGE ( 'NONE', *, *, #114378, .T. ) ;
#86468=EDGE_CURVE ( 'NONE', #31906, #141911, #40819, .T. ) ;
#86471=AXIS2_PLACEMENT_3D ( 'NONE', #108793, #31981, #8063 ) ;
#86472=VERTEX_POINT ( 'NONE', #106033 ) ;
#86473=CARTESIAN_POINT ( 'NONE',  ( -3.328169399223498637, -3.740707523384246613, 4.000000000000000000 ) ) ;
#86474=CARTESIAN_POINT ( 'NONE',  ( -2.999999999999981792, -0.8619312979532001151, -5.102805207349832450 ) ) ;
#86477=CARTESIAN_POINT ( 'NONE',  ( 18.29974487139159223, -27.71228299555219010, 4.000000000000000000 ) ) ;
#86479=ADVANCED_FACE ( 'NONE', ( #117618 ), #39403, .F. ) ;
#86481=DIRECTION ( 'NONE',  ( -0.7071067811865487940, 0.7071067811865463515, -0.000000000000000000 ) ) ;
#86483=VECTOR ( 'NONE', #10247, 999.9999999999998863 ) ;
#86485=CARTESIAN_POINT ( 'NONE',  ( 13.49999999999990408, -19.91253812416055879, 4.000000000000000000 ) ) ;
#86486=VECTOR ( 'NONE', #118751, 1000.000000000000227 ) ;
#86487=PLANE ( 'NONE',  #124674 ) ;
#86488=LINE ( 'NONE', #95194, #58362 ) ;
#86489=ORIENTED_EDGE ( 'NONE', *, *, #83638, .T. ) ;
#86491=CARTESIAN_POINT ( 'NONE',  ( 31.17183060077625356, 18.75929247661552068, 4.000000000000000000 ) ) ;
#86495=VECTOR ( 'NONE', #98384, 999.9999999999998863 ) ;
#86496=CARTESIAN_POINT ( 'NONE',  ( -31.49999999999977973, -11.94781430457070392, 5.000000000000000000 ) ) ;
#86497=EDGE_CURVE ( 'NONE', #110441, #91654, #51707, .T. ) ;
#86498=VERTEX_POINT ( 'NONE', #61193 ) ;
#86499=VERTEX_POINT ( 'NONE', #49584 ) ;
#86500=CARTESIAN_POINT ( 'NONE',  ( 75.18398860626899705, 28.73617430169839793, 5.000000000000000000 ) ) ;
#86501=EDGE_CURVE ( 'NONE', #123401, #72522, #82906, .T. ) ;
#86502=AXIS2_PLACEMENT_3D ( 'NONE', #121375, #54024, #11153 ) ;
#86503=ORIENTED_EDGE ( 'NONE', *, *, #125721, .F. ) ;
#86504=ORIENTED_EDGE ( 'NONE', *, *, #19150, .F. ) ;
#86506=CARTESIAN_POINT ( 'NONE',  ( 32.27718569542918203, -21.72500000000000142, 5.000000000000000000 ) ) ;
#86507=VERTEX_POINT ( 'NONE', #105344 ) ;
#86508=CARTESIAN_POINT ( 'NONE',  ( -19.05000000000000071, 3.174999999999997158, 5.000000000000000000 ) ) ;
#86509=VECTOR ( 'NONE', #37982, 1000.000000000000000 ) ;
#86510=CARTESIAN_POINT ( 'NONE',  ( 29.20710678118634007, 0.7592924766157052030, 5.000000000000000000 ) ) ;
#86511=EDGE_CURVE ( 'NONE', #11859, #80263, #94463, .T. ) ;
#86512=FACE_OUTER_BOUND ( 'NONE', #59202, .T. ) ;
#86513=DIRECTION ( 'NONE',  ( 0.7071067811865487940, 0.7071067811865463515, 0.000000000000000000 ) ) ;
#86514=ORIENTED_EDGE ( 'NONE', *, *, #117840, .F. ) ;
#86515=EDGE_CURVE ( 'NONE', #63026, #56797, #95179, .T. ) ;
#86516=LINE ( 'NONE', #9623, #141332 ) ;
#86518=DIRECTION ( 'NONE',  ( -0.7071067811865486830, -0.7071067811865464625, 0.000000000000000000 ) ) ;
#86519=LINE ( 'NONE', #110365, #50358 ) ;
#86520=CARTESIAN_POINT ( 'NONE',  ( 5.999999999999961808, -3.033600742197710254, 5.000000000000000000 ) ) ;
#86521=CARTESIAN_POINT ( 'NONE',  ( -22.49999999999983302, -1.912538124160733766, 4.000000000000000000 ) ) ;
#86522=VECTOR ( 'NONE', #10430, 1000.000000000000114 ) ;
#86525=CARTESIAN_POINT ( 'NONE',  ( -20.01844734635657730, 18.75929247661551713, 20.33588619593447433 ) ) ;
#86526=ORIENTED_EDGE ( 'NONE', *, *, #50816, .F. ) ;
#86527=ORIENTED_EDGE ( 'NONE', *, *, #109942, .T. ) ;
#86529=CARTESIAN_POINT ( 'NONE',  ( -57.18398860626899705, 28.73617430169827358, 5.000000000000000000 ) ) ;
#86530=DIRECTION ( 'NONE',  ( -0.000000000000000000, -0.3543493200069152693, 0.9351131265310292928 ) ) ;
#86533=ORIENTED_EDGE ( 'NONE', *, *, #25842, .T. ) ;
#86534=DIRECTION ( 'NONE',  ( 0.7071067811865487940, -0.7071067811865463515, 0.000000000000000000 ) ) ;
#86535=ADVANCED_FACE ( 'NONE', ( #16923 ), #84350, .F. ) ;
#86536=LINE ( 'NONE', #98115, #79371 ) ;
#86538=EDGE_LOOP ( 'NONE', ( #68551, #130607, #113881, #71854 ) ) ;
#86540=EDGE_LOOP ( 'NONE', ( #76312, #22833, #809, #22220 ) ) ;
#86541=ORIENTED_EDGE ( 'NONE', *, *, #22522, .F. ) ;
#86542=AXIS2_PLACEMENT_3D ( 'NONE', #64890, #22060, #75068 ) ;
#86544=DIRECTION ( 'NONE',  ( -1.000000000000000000, 0.000000000000000000, 0.000000000000000000 ) ) ;
#86545=LINE ( 'NONE', #53932, #30385 ) ;
#86546=LINE ( 'NONE', #77116, #101908 ) ;
#86548=DIRECTION ( 'NONE',  ( 0.7071067811865486830, -0.7071067811865464625, -0.000000000000000000 ) ) ;
#86552=DIRECTION ( 'NONE',  ( -0.7071067811865487940, 0.7071067811865463515, 0.000000000000000000 ) ) ;
#86553=CARTESIAN_POINT ( 'NONE',  ( -51.18398860626899705, 28.73617430169823095, 5.000000000000000000 ) ) ;
#86554=LINE ( 'NONE', #75672, #116332 ) ;
#86555=CARTESIAN_POINT ( 'NONE',  ( 10.49999999999992895, -20.56887692260759337, 4.000000000000000000 ) ) ;
#86556=DIRECTION ( 'NONE',  ( -1.000000000000000000, 2.775557561562888827E-14, 0.000000000000000000 ) ) ;
#86558=EDGE_LOOP ( 'NONE', ( #121578, #112913, #9392, #41076 ) ) ;
#86559=VECTOR ( 'NONE', #82502, 1000.000000000000000 ) ;
#86562=EDGE_CURVE ( 'NONE', #111382, #124741, #83636, .T. ) ;
#86563=LINE ( 'NONE', #109721, #101978 ) ;
#86564=LINE ( 'NONE', #139540, #22297 ) ;
#86565=PLANE ( 'NONE',  #108075 ) ;
#86566=ORIENTED_EDGE ( 'NONE', *, *, #64445, .F. ) ;
#86567=VERTEX_POINT ( 'NONE', #82212 ) ;
#86568=DIRECTION ( 'NONE',  ( -0.3543493200069162685, -0.000000000000000000, -0.9351131265310288487 ) ) ;
#86571=EDGE_CURVE ( 'NONE', #115190, #28781, #17607, .T. ) ;
#86573=VECTOR ( 'NONE', #133334, 1000.000000000000000 ) ;
#86574=EDGE_LOOP ( 'NONE', ( #72020, #20104, #93982, #105977 ) ) ;
#86576=VERTEX_POINT ( 'NONE', #85021 ) ;
#86577=CARTESIAN_POINT ( 'NONE',  ( -17.78795468754224629, 22.22500000000000142, -1.493867085284279028 ) ) ;
#86578=CARTESIAN_POINT ( 'NONE',  ( 6.005480084712508493, 28.92564299267933947, 4.000000000000000000 ) ) ;
#86579=CARTESIAN_POINT ( 'NONE',  ( -16.49999999999988276, 15.43112307739202471, 4.000000000000000000 ) ) ;
#86580=EDGE_CURVE ( 'NONE', #74550, #116562, #29211, .T. ) ;
#86581=FACE_BOUND ( 'NONE', #585, .T. ) ;
#86582=EDGE_CURVE ( 'NONE', #75761, #83246, #27071, .T. ) ;
#86584=PLANE ( 'NONE',  #67542 ) ;
#86585=CARTESIAN_POINT ( 'NONE',  ( 11.81601139373100651, 28.73617430169779041, 5.000000000000000000 ) ) ;
#86586=DIRECTION ( 'NONE',  ( -0.000000000000000000, -0.3543493200069152693, 0.9351131265310292928 ) ) ;
#86587=ORIENTED_EDGE ( 'NONE', *, *, #67699, .F. ) ;
#86588=AXIS2_PLACEMENT_3D ( 'NONE', #70059, #91748, #36652 ) ;
#86589=LINE ( 'NONE', #75705, #18491 ) ;
#86590=EDGE_CURVE ( 'NONE', #117979, #46897, #16165, .T. ) ;
#86591=VERTEX_POINT ( 'NONE', #25381 ) ;
#86593=ORIENTED_EDGE ( 'NONE', *, *, #47471, .F. ) ;
#86595=ORIENTED_EDGE ( 'NONE', *, *, #41759, .F. ) ;
#86596=FACE_OUTER_BOUND ( 'NONE', #135591, .T. ) ;
#86597=DIRECTION ( 'NONE',  ( 0.7071067811865487940, 0.7071067811865463515, -0.000000000000000000 ) ) ;
#86599=CARTESIAN_POINT ( 'NONE',  ( -23.36654548503486950, 7.297668562427137573, 4.000000000000000000 ) ) ;
#86600=EDGE_CURVE ( 'NONE', #123534, #84565, #102273, .T. ) ;
#86602=DIRECTION ( 'NONE',  ( -0.7071067811865486830, 0.7071067811865464625, 0.000000000000000000 ) ) ;
#86603=LINE ( 'NONE', #131520, #76129 ) ;
#86604=DIRECTION ( 'NONE',  ( 0.7071067811865487940, 0.7071067811865463515, -0.000000000000000000 ) ) ;
#86605=VECTOR ( 'NONE', #142280, 999.9999999999998863 ) ;
#86606=CARTESIAN_POINT ( 'NONE',  ( -9.489213562373095101, -27.52281430457062328, 5.000000000000000000 ) ) ;
#86607=LINE ( 'NONE', #31499, #137274 ) ;
#86608=CARTESIAN_POINT ( 'NONE',  ( 4.499999999999976019, -20.94781430457061333, 5.000000000000000000 ) ) ;
#86609=ORIENTED_EDGE ( 'NONE', *, *, #4997, .F. ) ;
#86610=EDGE_CURVE ( 'NONE', #52838, #13117, #36288, .T. ) ;
#86611=DIRECTION ( 'NONE',  ( -0.6830127018922180770, -0.6830127018922204085, -0.2588190451025213501 ) ) ;
#86612=VERTEX_POINT ( 'NONE', #38427 ) ;
#86614=DIRECTION ( 'NONE',  ( 0.7071067811865486830, -0.7071067811865464625, -0.000000000000000000 ) ) ;
#86615=AXIS2_PLACEMENT_3D ( 'NONE', #9589, #108175, #8840 ) ;
#86617=VERTEX_POINT ( 'NONE', #2173 ) ;
#86618=AXIS2_PLACEMENT_3D ( 'NONE', #114598, #3672, #135667 ) ;
#86619=ORIENTED_EDGE ( 'NONE', *, *, #95368, .F. ) ;
#86620=EDGE_CURVE ( 'NONE', #2255, #138900, #92069, .T. ) ;
#86622=ORIENTED_EDGE ( 'NONE', *, *, #13326, .T. ) ;
#86623=CARTESIAN_POINT ( 'NONE',  ( 0.000000000000000000, 0.000000000000000000, 5.000000000000000000 ) ) ;
#86625=AXIS2_PLACEMENT_3D ( 'NONE', #3802, #52170, #107257 ) ;
#86626=ADVANCED_FACE ( 'NONE', ( #58806 ), #104369, .F. ) ;
#86627=PLANE ( 'NONE',  #132648 ) ;
#86628=VECTOR ( 'NONE', #104625, 1000.000000000000000 ) ;
#86631=VERTEX_POINT ( 'NONE', #49330 ) ;
#86632=DIRECTION ( 'NONE',  ( 1.000000000000000000, 0.000000000000000000, 0.000000000000000000 ) ) ;
#86633=ORIENTED_EDGE ( 'NONE', *, *, #125074, .T. ) ;
#86634=FACE_OUTER_BOUND ( 'NONE', #78401, .T. ) ;
#86636=ORIENTED_EDGE ( 'NONE', *, *, #126985, .F. ) ;
#86637=ORIENTED_EDGE ( 'NONE', *, *, #2060, .F. ) ;
#86638=PLANE ( 'NONE',  #139924 ) ;
#86639=CARTESIAN_POINT ( 'NONE',  ( -24.27121408575940009, 22.22500000000000142, 9.037117742336768345 ) ) ;
#86640=CARTESIAN_POINT ( 'NONE',  ( 11.29320749275918701, 20.25929247661551358, 20.83292124670812129 ) ) ;
#86643=VERTEX_POINT ( 'NONE', #4286 ) ;
#86644=VERTEX_POINT ( 'NONE', #113832 ) ;
#86645=VERTEX_POINT ( 'NONE', #37725 ) ;
#86646=ADVANCED_FACE ( 'NONE', ( #80519 ), #115218, .F. ) ;
#86647=CARTESIAN_POINT ( 'NONE',  ( -33.18398860626899705, 28.73617430169810305, 5.000000000000000000 ) ) ;
#86650=DIRECTION ( 'NONE',  ( -0.3543493200069162685, -0.000000000000000000, -0.9351131265310288487 ) ) ;
#86652=CARTESIAN_POINT ( 'NONE',  ( -34.92500000000001847, 19.80009451602700210, 4.759050581649337808 ) ) ;
#86653=ORIENTED_EDGE ( 'NONE', *, *, #24956, .T. ) ;
#86654=ADVANCED_FACE ( 'NONE', ( #48584 ), #135602, .F. ) ;
#86655=CARTESIAN_POINT ( 'NONE',  ( -39.70679250724050746, 20.25929247661551358, 20.83292124670823853 ) ) ;
#86656=VERTEX_POINT ( 'NONE', #79835 ) ;
#86658=DIRECTION ( 'NONE',  ( 0.6830127018922181881, 0.6830127018922202975, -0.2588190451025214056 ) ) ;
#86659=EDGE_LOOP ( 'NONE', ( #90730, #81644, #11336, #94021 ) ) ;
#86660=CARTESIAN_POINT ( 'NONE',  ( 36.45983838949717892, 18.75929247661552779, 8.305906642995569911 ) ) ;
#86662=EDGE_LOOP ( 'NONE', ( #130242, #80005, #92263, #112956, #118517 ) ) ;
#86663=ORIENTED_EDGE ( 'NONE', *, *, #99609, .T. ) ;
#86664=LINE ( 'NONE', #19945, #139086 ) ;
#86666=DIRECTION ( 'NONE',  ( -0.7071067811865486830, -0.7071067811865464625, -0.000000000000000000 ) ) ;
#86668=FACE_OUTER_BOUND ( 'NONE', #2813, .T. ) ;
#86670=LINE ( 'NONE', #64916, #32602 ) ;
#86671=LINE ( 'NONE', #51903, #111000 ) ;
#86672=CARTESIAN_POINT ( 'NONE',  ( 15.18398860626900237, 28.73617430169797871, 5.000000000000000000 ) ) ;
#86673=CARTESIAN_POINT ( 'NONE',  ( 2.999999999999976463, 15.45873954670185846, -0.03131636524294698076 ) ) ;
#86674=ADVANCED_FACE ( 'NONE', ( #15209 ), #46493, .F. ) ;
#86675=VERTEX_POINT ( 'NONE', #134915 ) ;
#86676=CARTESIAN_POINT ( 'NONE',  ( -27.48921356237309155, -27.52281430457074762, 5.000000000000000000 ) ) ;
#86677=ORIENTED_EDGE ( 'NONE', *, *, #122579, .T. ) ;
#86679=LINE ( 'NONE', #63520, #100884 ) ;
#86680=EDGE_LOOP ( 'NONE', ( #64763, #36770, #138030, #86337 ) ) ;
#86681=DIRECTION ( 'NONE',  ( -8.817971600062199903E-18, 0.3543493200069153248, 0.9351131265310292928 ) ) ;
#86682=LINE ( 'NONE', #119967, #11826 ) ;
#86683=EDGE_LOOP ( 'NONE', ( #107102, #4155, #74688, #23675 ) ) ;
#86684=FACE_OUTER_BOUND ( 'NONE', #9943, .T. ) ;
#86685=EDGE_CURVE ( 'NONE', #52354, #12991, #114211, .T. ) ;
#86686=DIRECTION ( 'NONE',  ( 0.7071067811865487940, 0.7071067811865463515, 0.000000000000000000 ) ) ;
#86687=CARTESIAN_POINT ( 'NONE',  ( -5.510786437626906675, -27.52281430457051314, 5.000000000000000000 ) ) ;
#86688=ORIENTED_EDGE ( 'NONE', *, *, #56425, .T. ) ;
#86689=ADVANCED_FACE ( 'NONE', ( #59487 ), #93515, .F. ) ;
#86690=ORIENTED_EDGE ( 'NONE', *, *, #104586, .T. ) ;
#86691=LINE ( 'NONE', #31588, #62608 ) ;
#86692=CARTESIAN_POINT ( 'NONE',  ( -30.18398860626900060, 28.73617430169808173, 5.000000000000000000 ) ) ;
#86693=VECTOR ( 'NONE', #134398, 1000.000000000000000 ) ;
#86697=LINE ( 'NONE', #139668, #41665 ) ;
#86698=VECTOR ( 'NONE', #134869, 1000.000000000000000 ) ;
#86702=FACE_OUTER_BOUND ( 'NONE', #139699, .T. ) ;
#86705=CARTESIAN_POINT ( 'NONE',  ( 13.79551713769220811, 6.008391563887172993, 4.335713449946892339 ) ) ;
#86706=ORIENTED_EDGE ( 'NONE', *, *, #16527, .T. ) ;
#86707=EDGE_CURVE ( 'NONE', #71142, #22022, #36978, .T. ) ;
#86708=CARTESIAN_POINT ( 'NONE',  ( -51.18398860626899705, 28.73617430169823095, 5.000000000000000000 ) ) ;
#86709=ORIENTED_EDGE ( 'NONE', *, *, #79307, .F. ) ;
#86710=VECTOR ( 'NONE', #121738, 1000.000000000000000 ) ;
#86712=CARTESIAN_POINT ( 'NONE',  ( -66.48921356237309510, -27.52281430457101763, 5.000000000000000000 ) ) ;
#86713=CARTESIAN_POINT ( 'NONE',  ( 6.489213562373093325, -27.52281430457059841, 5.000000000000000000 ) ) ;
#86714=EDGE_LOOP ( 'NONE', ( #93512, #11273, #32901, #111223 ) ) ;
#86715=ADVANCED_FACE ( 'NONE', ( #57348 ), #101523, .F. ) ;
#86716=CARTESIAN_POINT ( 'NONE',  ( 7.499999999999952927, -4.912538124160708897, 4.000000000000000000 ) ) ;
#86717=LINE ( 'NONE', #75835, #53460 ) ;
#86718=LINE ( 'NONE', #87427, #37135 ) ;
#86719=DIRECTION ( 'NONE',  ( -0.7071067811865487940, 0.7071067811865463515, 0.000000000000000000 ) ) ;
#86720=DIRECTION ( 'NONE',  ( -0.6830127018922180770, 0.6830127018922202975, -0.2588190451025213501 ) ) ;
#86721=ORIENTED_EDGE ( 'NONE', *, *, #128418, .T. ) ;
#86725=VECTOR ( 'NONE', #127635, 1000.000000000000000 ) ;
#86726=ORIENTED_EDGE ( 'NONE', *, *, #70071, .T. ) ;
#86727=ORIENTED_EDGE ( 'NONE', *, *, #131427, .T. ) ;
#86729=VECTOR ( 'NONE', #40809, 1000.000000000000000 ) ;
#86730=VECTOR ( 'NONE', #15108, 1000.000000000000227 ) ;
#86731=ORIENTED_EDGE ( 'NONE', *, *, #51867, .F. ) ;
#86733=ADVANCED_FACE ( 'NONE', ( #68938 ), #13775, .F. ) ;
#86736=FACE_OUTER_BOUND ( 'NONE', #127564, .T. ) ;
#86737=ORIENTED_EDGE ( 'NONE', *, *, #104971, .T. ) ;
#86738=DIRECTION ( 'NONE',  ( -0.000000000000000000, 0.3543493200069153248, 0.9351131265310292928 ) ) ;
#86739=DIRECTION ( 'NONE',  ( -0.7071067811865486830, -0.7071067811865464625, 0.000000000000000000 ) ) ;
#86740=EDGE_CURVE ( 'NONE', #42201, #99199, #40977, .T. ) ;
#86741=ADVANCED_FACE ( 'NONE', ( #141731 ), #98217, .F. ) ;
#86742=VERTEX_POINT ( 'NONE', #108324 ) ;
#86743=CARTESIAN_POINT ( 'NONE',  ( -34.92500000000001137, -22.22500000000000142, 4.500000000000000888 ) ) ;
#86744=CARTESIAN_POINT ( 'NONE',  ( 23.99999999999984013, -1.447814304570811617, 5.000000000000000000 ) ) ;
#86745=CARTESIAN_POINT ( 'NONE',  ( -8.292986735706895374, -21.74070752338406010, 4.999753212805224223 ) ) ;
#86746=EDGE_CURVE ( 'NONE', #96318, #138853, #42431, .T. ) ;
#86748=ORIENTED_EDGE ( 'NONE', *, *, #43969, .F. ) ;
#86749=EDGE_CURVE ( 'NONE', #135705, #75982, #12376, .T. ) ;
#86750=FACE_BOUND ( 'NONE', #31791, .T. ) ;
#86751=EDGE_CURVE ( 'NONE', #6180, #55828, #109796, .T. ) ;
#86752=FACE_OUTER_BOUND ( 'NONE', #8880, .T. ) ;
#86753=DIRECTION ( 'NONE',  ( -0.7071067811865486830, -0.7071067811865464625, 0.000000000000000000 ) ) ;
#86754=DIRECTION ( 'NONE',  ( -0.7071067811865486830, -0.7071067811865464625, 0.000000000000000000 ) ) ;
#86755=CARTESIAN_POINT ( 'NONE',  ( -24.48921356237309510, -27.52281430457072631, 5.000000000000000000 ) ) ;
#86757=ORIENTED_EDGE ( 'NONE', *, *, #139122, .F. ) ;
#86758=EDGE_CURVE ( 'NONE', #45664, #80973, #30834, .T. ) ;
#86759=ORIENTED_EDGE ( 'NONE', *, *, #49939, .T. ) ;
#86761=ORIENTED_EDGE ( 'NONE', *, *, #9622, .T. ) ;
#86762=ADVANCED_FACE ( 'NONE', ( #22056 ), #140977, .T. ) ;
#86763=ORIENTED_EDGE ( 'NONE', *, *, #79755, .F. ) ;
#86765=EDGE_CURVE ( 'NONE', #95628, #270, #130138, .T. ) ;
#86766=CARTESIAN_POINT ( 'NONE',  ( 15.51665438641034633, 22.22500000000000142, 4.500000000000000888 ) ) ;
#86767=CARTESIAN_POINT ( 'NONE',  ( -29.99999999999978328, -22.22500000000000853, 4.412002311790081954 ) ) ;
#86768=VERTEX_POINT ( 'NONE', #109064 ) ;
#86770=CARTESIAN_POINT ( 'NONE',  ( 38.99451991528749062, 28.92564299267965211, 4.000000000000000000 ) ) ;
#86771=CARTESIAN_POINT ( 'NONE',  ( -38.99451991528749062, 28.92564299267965211, 4.000000000000000000 ) ) ;
#86772=CARTESIAN_POINT ( 'NONE',  ( 33.18398860626899705, 28.73617430169810305, 5.000000000000000000 ) ) ;
#86773=CARTESIAN_POINT ( 'NONE',  ( -32.67183060077624646, -15.74070752338412404, 4.000000000000000000 ) ) ;
#86774=EDGE_CURVE ( 'NONE', #55801, #12165, #98902, .T. ) ;
#86775=DIRECTION ( 'NONE',  ( 0.7071067811865487940, 0.7071067811865463515, 0.000000000000000000 ) ) ;
#86776=EDGE_LOOP ( 'NONE', ( #54408, #122455, #99333, #129766 ) ) ;
#86777=DIRECTION ( 'NONE',  ( 0.7071067811865487940, 0.7071067811865463515, -0.000000000000000000 ) ) ;
#86779=ORIENTED_EDGE ( 'NONE', *, *, #133996, .F. ) ;
#86780=CARTESIAN_POINT ( 'NONE',  ( -25.00442415654155681, 3.591886032380943838, 4.000000000000000000 ) ) ;
#86781=EDGE_LOOP ( 'NONE', ( #37007, #80620, #74846, #114926 ) ) ;
#86783=ORIENTED_EDGE ( 'NONE', *, *, #115823, .F. ) ;
#86785=EDGE_CURVE ( 'NONE', #18390, #42437, #10463, .T. ) ;
#86786=ORIENTED_EDGE ( 'NONE', *, *, #57784, .T. ) ;
#86787=ORIENTED_EDGE ( 'NONE', *, *, #58039, .F. ) ;
#86788=LINE ( 'NONE', #54879, #109153 ) ;
#86789=EDGE_CURVE ( 'NONE', #99104, #10403, #135164, .T. ) ;
#86794=DIRECTION ( 'NONE',  ( -0.7071067811865487940, 0.7071067811865463515, 0.000000000000000000 ) ) ;
#86796=LINE ( 'NONE', #109952, #129706 ) ;
#86797=ADVANCED_FACE ( 'NONE', ( #53256 ), #66312, .F. ) ;
#86798=DIRECTION ( 'NONE',  ( 0.7071067811865487940, 0.7071067811865463515, 0.000000000000000000 ) ) ;
#86801=EDGE_LOOP ( 'NONE', ( #34688, #18745, #50430, #49783 ) ) ;
#86802=CARTESIAN_POINT ( 'NONE',  ( 42.29974487139158157, -27.71228299555235708, 4.000000000000000000 ) ) ;
#86803=ORIENTED_EDGE ( 'NONE', *, *, #84594, .T. ) ;
#86804=ORIENTED_EDGE ( 'NONE', *, *, #120403, .F. ) ;
#86805=ORIENTED_EDGE ( 'NONE', *, *, #119718, .T. ) ;
#86807=VERTEX_POINT ( 'NONE', #32241 ) ;
#86808=LINE ( 'NONE', #31704, #79301 ) ;
#86809=FACE_OUTER_BOUND ( 'NONE', #38649, .T. ) ;
#86810=VERTEX_POINT ( 'NONE', #9757 ) ;
#86811=LINE ( 'NONE', #64453, #19655 ) ;
#86812=DIRECTION ( 'NONE',  ( -0.7071067811865487940, 0.7071067811865463515, 0.000000000000000000 ) ) ;
#86814=VECTOR ( 'NONE', #104690, 1000.000000000000000 ) ;
#86815=AXIS2_PLACEMENT_3D ( 'NONE', #11882, #78596, #113338 ) ;
#86817=DIRECTION ( 'NONE',  ( -0.000000000000000000, 0.3543493200069153248, 0.9351131265310292928 ) ) ;
#86818=AXIS2_PLACEMENT_3D ( 'NONE', #128169, #107098, #128852 ) ;
#86819=DIRECTION ( 'NONE',  ( -0.7071067811865486830, 0.7071067811865464625, 0.000000000000000000 ) ) ;
#86820=AXIS2_PLACEMENT_3D ( 'NONE', #22342, #110781, #44902 ) ;
#86821=CARTESIAN_POINT ( 'NONE',  ( -31.49999999999977973, 5.696342897626483825, -7.587980461218473138 ) ) ;
#86822=ORIENTED_EDGE ( 'NONE', *, *, #78765, .T. ) ;
#86823=EDGE_LOOP ( 'NONE', ( #39579, #45725, #84631, #90659, #95519, #37062 ) ) ;
#86824=EDGE_CURVE ( 'NONE', #70917, #37150, #1712, .T. ) ;
#86825=ADVANCED_FACE ( 'NONE', ( #76478 ), #110483, .F. ) ;
#86826=EDGE_LOOP ( 'NONE', ( #72398, #138979, #132304, #103121 ) ) ;
#86827=DIRECTION ( 'NONE',  ( 0.7071067811865487940, -0.7071067811865463515, 0.000000000000000000 ) ) ;
#86830=CARTESIAN_POINT ( 'NONE',  ( -30.18398860626900060, 28.73617430169808173, 5.000000000000000000 ) ) ;
#86831=DIRECTION ( 'NONE',  ( -0.000000000000000000, -0.3543493200069152693, 0.9351131265310292928 ) ) ;
#86832=CARTESIAN_POINT ( 'NONE',  ( 19.05000000000000071, 3.174999999999997158, 4.000000000000000000 ) ) ;
#86834=LINE ( 'NONE', #139808, #141628 ) ;
#86835=DIRECTION ( 'NONE',  ( 0.7071067811865487940, 0.7071067811865463515, 0.000000000000000000 ) ) ;
#86836=ORIENTED_EDGE ( 'NONE', *, *, #16416, .F. ) ;
#86837=DIRECTION ( 'NONE',  ( 0.7071067811865487940, 0.7071067811865463515, -0.000000000000000000 ) ) ;
#86838=ORIENTED_EDGE ( 'NONE', *, *, #76217, .T. ) ;
#86839=DIRECTION ( 'NONE',  ( 0.6830127018922180770, -0.6830127018922204085, -0.2588190451025213501 ) ) ;
#86840=ORIENTED_EDGE ( 'NONE', *, *, #42750, .F. ) ;
#86841=EDGE_CURVE ( 'NONE', #40570, #27504, #63477, .T. ) ;
#86842=CARTESIAN_POINT ( 'NONE',  ( 18.18398860626898994, 28.73617430169800002, 5.000000000000000000 ) ) ;
#86843=DIRECTION ( 'NONE',  ( 1.000000000000000000, 0.000000000000000000, 0.000000000000000000 ) ) ;
#86844=ORIENTED_EDGE ( 'NONE', *, *, #25023, .T. ) ;
#86845=ADVANCED_FACE ( 'NONE', ( #111955 ), #135154, .F. ) ;
#86846=DIRECTION ( 'NONE',  ( 0.7071067811865487940, 0.7071067811865463515, 0.000000000000000000 ) ) ;
#86847=EDGE_LOOP ( 'NONE', ( #47067, #43821, #46872, #106604 ) ) ;
#86848=CARTESIAN_POINT ( 'NONE',  ( 34.49999999999975842, -4.216083040037219121, -7.486842126848736179 ) ) ;
#86849=EDGE_LOOP ( 'NONE', ( #51343, #99467, #137933, #63617 ) ) ;
#86850=DIRECTION ( 'NONE',  ( -1.000000000000000000, 1.743732761913359971E-15, 0.000000000000000000 ) ) ;
#86852=VERTEX_POINT ( 'NONE', #78601 ) ;
#86853=EDGE_CURVE ( 'NONE', #92018, #42749, #46744, .T. ) ;
#86855=DIRECTION ( 'NONE',  ( -0.7071067811865486830, -0.7071067811865464625, 0.000000000000000000 ) ) ;
#86857=DIRECTION ( 'NONE',  ( -0.7071067811865486830, -0.7071067811865464625, -0.000000000000000000 ) ) ;
#86858=CARTESIAN_POINT ( 'NONE',  ( -39.18398860626899705, 28.73617430169814568, 5.000000000000000000 ) ) ;
#86859=ADVANCED_FACE ( 'NONE', ( #69166 ), #35848, .F. ) ;
#86860=CARTESIAN_POINT ( 'NONE',  ( 9.005480084712511157, 28.92564299267931816, 4.000000000000000000 ) ) ;
#86861=CARTESIAN_POINT ( 'NONE',  ( -20.29387692260790388, 22.22500000000000142, 4.000000000000000000 ) ) ;
#86862=FACE_OUTER_BOUND ( 'NONE', #76746, .T. ) ;
#86865=LINE ( 'NONE', #44073, #18797 ) ;
#86867=EDGE_LOOP ( 'NONE', ( #49996, #45416, #86938, #19498 ) ) ;
#86868=ORIENTED_EDGE ( 'NONE', *, *, #41566, .F. ) ;
#86869=EDGE_CURVE ( 'NONE', #109420, #61439, #14031, .T. ) ;
#86870=FACE_OUTER_BOUND ( 'NONE', #38975, .T. ) ;
#86871=ORIENTED_EDGE ( 'NONE', *, *, #127346, .T. ) ;
#86872=CARTESIAN_POINT ( 'NONE',  ( 18.66846741159845635, -18.74070752338408852, 20.73178291233845627 ) ) ;
#86873=CARTESIAN_POINT ( 'NONE',  ( -27.18398860626900060, 28.73617430169806042, 5.000000000000000000 ) ) ;
#86874=ORIENTED_EDGE ( 'NONE', *, *, #51874, .F. ) ;
#86875=EDGE_CURVE ( 'NONE', #110155, #57989, #101047, .T. ) ;
#86876=CARTESIAN_POINT ( 'NONE',  ( 31.49999999999978684, 0.4497235411627769075, -5.599840258123467862 ) ) ;
#86877=DIRECTION ( 'NONE',  ( -0.7071067811865486830, 0.7071067811865464625, 0.000000000000000000 ) ) ;
#86880=CARTESIAN_POINT ( 'NONE',  ( 14.24715658456393541, 6.719242673238161601, 5.000000000000000000 ) ) ;
#86881=DIRECTION ( 'NONE',  ( -0.7071067811865486830, 0.7071067811865464625, 0.000000000000000000 ) ) ;
#86882=EDGE_LOOP ( 'NONE', ( #30915, #67307, #122796, #17604 ) ) ;
#86883=CARTESIAN_POINT ( 'NONE',  ( -11.99999999999991296, -5.527737879153202805, -7.983877177622344057 ) ) ;
#86887=ADVANCED_FACE ( 'NONE', ( #124241 ), #45997, .T. ) ;
#86888=DIRECTION ( 'NONE',  ( -0.000000000000000000, -0.3543493200069152693, 0.9351131265310292928 ) ) ;
#86889=CARTESIAN_POINT ( 'NONE',  ( 34.49999999999975842, -7.535744391599426883, 4.994342998332164107 ) ) ;
#86890=VERTEX_POINT ( 'NONE', #35121 ) ;
#86892=ORIENTED_EDGE ( 'NONE', *, *, #91337, .T. ) ;
#86893=EDGE_LOOP ( 'NONE', ( #61106, #103793, #91308, #8116 ) ) ;
#86895=ORIENTED_EDGE ( 'NONE', *, *, #7200, .T. ) ;
#86896=EDGE_CURVE ( 'NONE', #83442, #12698, #79364, .T. ) ;
#86897=CARTESIAN_POINT ( 'NONE',  ( 25.49999999999982947, -13.53360074219759746, 5.000000000000000000 ) ) ;
#86898=CARTESIAN_POINT ( 'NONE',  ( -5.999999999999956479, 7.007997736742436423, -8.085015511992127202 ) ) ;
#86899=ORIENTED_EDGE ( 'NONE', *, *, #74720, .F. ) ;
#86900=CARTESIAN_POINT ( 'NONE',  ( 23.29289321881330110, -9.740707523384184441, 5.000000000000000000 ) ) ;
#86902=ADVANCED_FACE ( 'NONE', ( #102514 ), #122812, .T. ) ;
#86903=EDGE_CURVE ( 'NONE', #105802, #95196, #133703, .T. ) ;
#86906=ORIENTED_EDGE ( 'NONE', *, *, #77346, .F. ) ;
#86907=EDGE_CURVE ( 'NONE', #66460, #114269, #135835, .T. ) ;
#86909=CARTESIAN_POINT ( 'NONE',  ( 7.499999999999951150, -10.53360074219763298, 5.000000000000000000 ) ) ;
#86911=VERTEX_POINT ( 'NONE', #123566 ) ;
#86912=ORIENTED_EDGE ( 'NONE', *, *, #78191, .F. ) ;
#86913=ORIENTED_EDGE ( 'NONE', *, *, #40741, .T. ) ;
#86914=LINE ( 'NONE', #52132, #100117 ) ;
#86915=EDGE_CURVE ( 'NONE', #109521, #89318, #56178, .T. ) ;
#86916=CARTESIAN_POINT ( 'NONE',  ( -51.48921356237309510, -27.52281430457091460, 5.000000000000000000 ) ) ;
#86918=CARTESIAN_POINT ( 'NONE',  ( 30.70710678118633652, 14.25929247661556509, 5.000000000000000000 ) ) ;
#86921=CARTESIAN_POINT ( 'NONE',  ( -8.816011393731004731, 28.73617430169781173, 5.000000000000000000 ) ) ;
#86922=SURFACE_STYLE_USAGE ( .BOTH. , #33293 ) ;
#86924=ORIENTED_EDGE ( 'NONE', *, *, #61807, .F. ) ;
#86925=VECTOR ( 'NONE', #126027, 1000.000000000000227 ) ;
#86926=ORIENTED_EDGE ( 'NONE', *, *, #119227, .F. ) ;
#86927=EDGE_CURVE ( 'NONE', #8502, #80270, #112651, .T. ) ;
#86928=LINE ( 'NONE', #122376, #22501 ) ;
#86929=ORIENTED_EDGE ( 'NONE', *, *, #20429, .T. ) ;
#86930=ORIENTED_EDGE ( 'NONE', *, *, #25339, .T. ) ;
#86931=EDGE_CURVE ( 'NONE', #123040, #112560, #69909, .T. ) ;
#86932=CARTESIAN_POINT ( 'NONE',  ( 15.19713381108422290, 7.733989266307781385, 4.000000000000000000 ) ) ;
#86933=ORIENTED_EDGE ( 'NONE', *, *, #59820, .F. ) ;
#86934=FACE_OUTER_BOUND ( 'NONE', #31206, .T. ) ;
#86935=LINE ( 'NONE', #55029, #71057 ) ;
#86936=PLANE ( 'NONE',  #18235 ) ;
#86938=ORIENTED_EDGE ( 'NONE', *, *, #9604, .T. ) ;
#86939=EDGE_LOOP ( 'NONE', ( #59243, #20952, #89659, #31965 ) ) ;
#86940=CARTESIAN_POINT ( 'NONE',  ( 51.18398860626899705, 28.73617430169823095, 5.000000000000000000 ) ) ;
#86941=VERTEX_POINT ( 'NONE', #77891 ) ;
#86942=LINE ( 'NONE', #95658, #104761 ) ;
#86943=ORIENTED_EDGE ( 'NONE', *, *, #49619, .T. ) ;
#86944=CARTESIAN_POINT ( 'NONE',  ( -34.92500000000001137, -17.14387692260738305, 4.000000000000000000 ) ) ;
#86945=VERTEX_POINT ( 'NONE', #287 ) ;
#86946=ORIENTED_EDGE ( 'NONE', *, *, #117277, .T. ) ;
#86947=ORIENTED_EDGE ( 'NONE', *, *, #102830, .F. ) ;
#86948=EDGE_CURVE ( 'NONE', #47328, #22343, #1011, .T. ) ;
#86951=DIRECTION ( 'NONE',  ( 0.7071067811865487940, -0.7071067811865463515, 0.000000000000000000 ) ) ;
#86953=DIRECTION ( 'NONE',  ( -0.7071067811865487940, 0.7071067811865463515, -0.000000000000000000 ) ) ;
#86954=CARTESIAN_POINT ( 'NONE',  ( -0.4892135623730947680, -27.52281430457055578, 5.000000000000000000 ) ) ;
#86955=DIRECTION ( 'NONE',  ( -0.3543493200069162685, -0.000000000000000000, -0.9351131265310288487 ) ) ;
#86956=CARTESIAN_POINT ( 'NONE',  ( -9.717577386425604757, -21.73023691814493574, 5.000000000000000888 ) ) ;
#86957=DIRECTION ( 'NONE',  ( 0.7071067811865487940, 0.7071067811865463515, 0.000000000000000000 ) ) ;
#86959=DIRECTION ( 'NONE',  ( 0.3543493200069162685, -0.000000000000000000, -0.9351131265310288487 ) ) ;
#86960=ORIENTED_EDGE ( 'NONE', *, *, #140707, .F. ) ;
#86961=ORIENTED_EDGE ( 'NONE', *, *, #105187, .F. ) ;
#86962=ORIENTED_EDGE ( 'NONE', *, *, #24266, .T. ) ;
#86963=DIRECTION ( 'NONE',  ( 0.7071067811865486830, -0.7071067811865464625, -0.000000000000000000 ) ) ;
#86965=ORIENTED_EDGE ( 'NONE', *, *, #20569, .T. ) ;
#86966=PLANE ( 'NONE',  #23572 ) ;
#86967=CARTESIAN_POINT ( 'NONE',  ( 44.99451991528749772, 28.92564299267969474, 4.000000000000000000 ) ) ;
#86968=DIRECTION ( 'NONE',  ( -0.3543493200069163240, -0.000000000000000000, 0.9351131265310288487 ) ) ;
#86969=ORIENTED_EDGE ( 'NONE', *, *, #110611, .T. ) ;
#86970=CARTESIAN_POINT ( 'NONE',  ( 47.99451991528749062, 28.92564299267971251, 4.000000000000000000 ) ) ;
#86971=EDGE_LOOP ( 'NONE', ( #84186, #97150, #95863 ) ) ;
#86972=CARTESIAN_POINT ( 'NONE',  ( 19.49999999999986855, 13.46639925780212010, 5.000000000000000000 ) ) ;
#86975=VERTEX_POINT ( 'NONE', #71309 ) ;
#86977=( BOUNDED_CURVE ( )  B_SPLINE_CURVE ( 3, ( #108453, #64290, #97607, #86766 ),
 .UNSPECIFIED., .F., .T. ) 
 B_SPLINE_CURVE_WITH_KNOTS ( ( 4, 4 ),
 ( 2.001653308786169649, 3.503810798801450854 ),
 .UNSPECIFIED. ) 
 CURVE ( )  GEOMETRIC_REPRESENTATION_ITEM ( )  RATIONAL_B_SPLINE_CURVE ( ( 1.000000000000000000, 0.8206354192515240564, 0.8206354192515240564, 1.000000000000000000 ) ) 
 REPRESENTATION_ITEM ( '' )  );
#86978=CARTESIAN_POINT ( 'NONE',  ( 26.51078643762690845, -27.52281430457036748, 5.000000000000000000 ) ) ;
#86979=VECTOR ( 'NONE', #91023, 1000.000000000000000 ) ;
#86982=VERTEX_POINT ( 'NONE', #125689 ) ;
#86983=ORIENTED_EDGE ( 'NONE', *, *, #52725, .F. ) ;
#86984=CARTESIAN_POINT ( 'NONE',  ( -62.99451991528749772, 28.92564299267982264, 4.000000000000000000 ) ) ;
#86985=EDGE_LOOP ( 'NONE', ( #65801, #18112, #126548, #39947 ) ) ;
#86986=CARTESIAN_POINT ( 'NONE',  ( 42.48921356237308800, -27.52281430457085065, 5.000000000000000000 ) ) ;
#86987=DIRECTION ( 'NONE',  ( 0.7071067811865487940, 0.7071067811865463515, 0.000000000000000000 ) ) ;
#86988=DIRECTION ( 'NONE',  ( 0.6830127018922180770, -0.6830127018922204085, -0.2588190451025213501 ) ) ;
#86990=VERTEX_POINT ( 'NONE', #115464 ) ;
#86991=DIRECTION ( 'NONE',  ( -0.7071067811865486830, 0.7071067811865464625, 0.000000000000000000 ) ) ;
#86992=LINE ( 'NONE', #40650, #60520 ) ;
#86993=DIRECTION ( 'NONE',  ( 0.7071067811865487940, -0.7071067811865463515, 0.000000000000000000 ) ) ;
#86994=EDGE_CURVE ( 'NONE', #40996, #135817, #28518, .T. ) ;
#86995=ORIENTED_EDGE ( 'NONE', *, *, #69198, .F. ) ;
#86997=PLANE ( 'NONE',  #79469 ) ;
#86998=ORIENTED_EDGE ( 'NONE', *, *, #22193, .F. ) ;
#87000=DIRECTION ( 'NONE',  ( 0.7071067811865487940, -0.7071067811865463515, 0.000000000000000000 ) ) ;
#87001=EDGE_LOOP ( 'NONE', ( #10251, #115625, #51521, #71151 ) ) ;
#87002=ORIENTED_EDGE ( 'NONE', *, *, #53571, .T. ) ;
#87003=EDGE_CURVE ( 'NONE', #39324, #35758, #137987, .T. ) ;
#87005=LINE ( 'NONE', #76138, #107193 ) ;
#87006=PLANE ( 'NONE',  #117810 ) ;
#87007=ORIENTED_EDGE ( 'NONE', *, *, #130310, .F. ) ;
#87008=CARTESIAN_POINT ( 'NONE',  ( 31.49999999999977973, -4.216083040037219121, -7.486842126848729073 ) ) ;
#87010=AXIS2_PLACEMENT_3D ( 'NONE', #114161, #39481, #138794 ) ;
#87011=ADVANCED_FACE ( 'NONE', ( #128537 ), #15437, .T. ) ;
#87013=CARTESIAN_POINT ( 'NONE',  ( -15.00548008471250228, 28.92564299267927552, 4.000000000000000000 ) ) ;
#87014=AXIS2_PLACEMENT_3D ( 'NONE', #7346, #129143, #60353 ) ;
#87015=LINE ( 'NONE', #21026, #43855 ) ;
#87016=VECTOR ( 'NONE', #87296, 999.9999999999998863 ) ;
#87019=VECTOR ( 'NONE', #102932, 1000.000000000000000 ) ;
#87020=ADVANCED_FACE ( 'NONE', ( #82898 ), #37234, .F. ) ;
#87021=LINE ( 'NONE', #31225, #76933 ) ;
#87022=CARTESIAN_POINT ( 'NONE',  ( -19.05000000000000071, 3.174999999999997158, 4.000000000000000000 ) ) ;
#87023=PLANE ( 'NONE',  #22837 ) ;
#87024=LINE ( 'NONE', #10163, #98885 ) ;
#87025=DIRECTION ( 'NONE',  ( -0.7071067811865486830, 0.7071067811865464625, 0.000000000000000000 ) ) ;
#87026=FACE_OUTER_BOUND ( 'NONE', #7956, .T. ) ;
#87028=ADVANCED_FACE ( 'NONE', ( #95169 ), #82203, .F. ) ;
#87029=CARTESIAN_POINT ( 'NONE',  ( -34.47516574401892342, 7.490517612115540125, 4.998110765256834398 ) ) ;
#87030=DIRECTION ( 'NONE',  ( 0.7071067811865486830, -0.7071067811865464625, -0.000000000000000000 ) ) ;
#87031=ORIENTED_EDGE ( 'NONE', *, *, #73257, .F. ) ;
#87032=ORIENTED_EDGE ( 'NONE', *, *, #26801, .T. ) ;
#87035=ADVANCED_FACE ( 'NONE', ( #138708 ), #27062, .T. ) ;
#87036=VERTEX_POINT ( 'NONE', #29204 ) ;
#87037=ORIENTED_EDGE ( 'NONE', *, *, #6613, .F. ) ;
#87038=ORIENTED_EDGE ( 'NONE', *, *, #35906, .F. ) ;
#87039=DIRECTION ( 'NONE',  ( 0.7071067811865486830, -0.7071067811865464625, -0.000000000000000000 ) ) ;
#87041=VERTEX_POINT ( 'NONE', #27779 ) ;
#87042=LINE ( 'NONE', #43534, #143516 ) ;
#87043=EDGE_CURVE ( 'NONE', #82254, #63910, #127834, .T. ) ;
#87044=LINE ( 'NONE', #133416, #132074 ) ;
#87045=CARTESIAN_POINT ( 'NONE',  ( 13.10530833935383299, 3.713635273109022084, 4.055062020558137803 ) ) ;
#87046=DIRECTION ( 'NONE',  ( 0.3543493200069163240, 0.000000000000000000, 0.9351131265310288487 ) ) ;
#87047=VERTEX_POINT ( 'NONE', #48841 ) ;
#87048=CARTESIAN_POINT ( 'NONE',  ( 0.000000000000000000, 0.000000000000000000, 5.000000000000000000 ) ) ;
#87049=DIRECTION ( 'NONE',  ( -0.000000000000000000, -0.3543493200069152693, 0.9351131265310292928 ) ) ;
#87050=LINE ( 'NONE', #79793, #21587 ) ;
#87052=FACE_OUTER_BOUND ( 'NONE', #140352, .T. ) ;
#87053=DIRECTION ( 'NONE',  ( 1.000000000000000000, 0.000000000000000000, 0.000000000000000000 ) ) ;
#87054=CARTESIAN_POINT ( 'NONE',  ( 23.99999999999983302, -18.41253812416056590, 4.000000000000000000 ) ) ;
#87056=( BOUNDED_CURVE ( )  B_SPLINE_CURVE ( 3, ( #118401, #52432, #116980, #116276 ),
 .UNSPECIFIED., .F., .T. ) 
 B_SPLINE_CURVE_WITH_KNOTS ( ( 4, 4 ),
 ( 1.208578181583237710, 1.359146454359470901 ),
 .UNSPECIFIED. ) 
 CURVE ( )  GEOMETRIC_REPRESENTATION_ITEM ( )  RATIONAL_B_SPLINE_CURVE ( ( 1.000000000000000000, 0.9981116584018945304, 0.9981116584018945304, 1.000000000000000000 ) ) 
 REPRESENTATION_ITEM ( '' )  );
#87057=CARTESIAN_POINT ( 'NONE',  ( -60.29974487139158867, -27.71228299555248142, 4.000000000000000000 ) ) ;
#87058=ORIENTED_EDGE ( 'NONE', *, *, #133187, .F. ) ;
#87059=ORIENTED_EDGE ( 'NONE', *, *, #35912, .F. ) ;
#87061=ORIENTED_EDGE ( 'NONE', *, *, #138241, .T. ) ;
#87062=FACE_OUTER_BOUND ( 'NONE', #71042, .T. ) ;
#87063=EDGE_CURVE ( 'NONE', #106536, #124008, #48123, .T. ) ;
#87064=FACE_OUTER_BOUND ( 'NONE', #4444, .T. ) ;
#87067=LINE ( 'NONE', #74791, #72430 ) ;
#87068=CARTESIAN_POINT ( 'NONE',  ( 10.49999999999992895, 14.14708470758592185, -0.5283514160166801199 ) ) ;
#87072=ORIENTED_EDGE ( 'NONE', *, *, #69567, .T. ) ;
#87073=EDGE_CURVE ( 'NONE', #6574, #76267, #140137, .T. ) ;
#87074=ORIENTED_EDGE ( 'NONE', *, *, #43504, .T. ) ;
#87075=FACE_OUTER_BOUND ( 'NONE', #56897, .T. ) ;
#87077=DIRECTION ( 'NONE',  ( -0.3543493200069162685, -0.000000000000000000, -0.9351131265310288487 ) ) ;
#87078=EDGE_CURVE ( 'NONE', #12722, #102325, #129221, .T. ) ;
#87079=CARTESIAN_POINT ( 'NONE',  ( -22.42820000000000036, 3.174999999999997602, 1.444000000000000394 ) ) ;
#87080=ORIENTED_EDGE ( 'NONE', *, *, #26447, .T. ) ;
#87082=ORIENTED_EDGE ( 'NONE', *, *, #56396, .F. ) ;
#87083=CARTESIAN_POINT ( 'NONE',  ( 29.99451991528749417, 28.92564299267958816, 4.000000000000000000 ) ) ;
#87084=LINE ( 'NONE', #131298, #120197 ) ;
#87085=DIRECTION ( 'NONE',  ( 0.7071067811865486830, -0.7071067811865464625, -0.000000000000000000 ) ) ;
#87087=EDGE_CURVE ( 'NONE', #106603, #126942, #98734, .T. ) ;
#87088=AXIS2_PLACEMENT_3D ( 'NONE', #51462, #28987, #77350 ) ;
#87090=EDGE_LOOP ( 'NONE', ( #16580, #60875, #41025, #671 ) ) ;
#87091=VECTOR ( 'NONE', #28962, 1000.000000000000000 ) ;
#87093=CARTESIAN_POINT ( 'NONE',  ( -12.88837638105233552, 9.759292476615614831, 17.35367589129215560 ) ) ;
#87094=ORIENTED_EDGE ( 'NONE', *, *, #111117, .F. ) ;
#87095=ORIENTED_EDGE ( 'NONE', *, *, #97281, .F. ) ;
#87096=ORIENTED_EDGE ( 'NONE', *, *, #15685, .T. ) ;
#87098=CARTESIAN_POINT ( 'NONE',  ( -0.4892135623730947680, -27.52281430457055578, 5.000000000000000000 ) ) ;
#87099=VERTEX_POINT ( 'NONE', #77031 ) ;
#87100=DIRECTION ( 'NONE',  ( 0.3543493200069162685, -0.000000000000000000, -0.9351131265310288487 ) ) ;
#87101=CARTESIAN_POINT ( 'NONE',  ( 15.48921356237309510, -27.52281430457066236, 5.000000000000000000 ) ) ;
#87102=CARTESIAN_POINT ( 'NONE',  ( 0.000000000000000000, 0.000000000000000000, 5.000000000000000000 ) ) ;
#87103=PLANE ( 'NONE',  #120730 ) ;
#87104=ADVANCED_FACE ( 'NONE', ( #42255 ), #29911, .F. ) ;
#87105=VECTOR ( 'NONE', #65890, 1000.000000000000000 ) ;
#87106=FACE_BOUND ( 'NONE', #103734, .T. ) ;
#87107=ORIENTED_EDGE ( 'NONE', *, *, #21447, .F. ) ;
#87108=DIRECTION ( 'NONE',  ( -0.7071067811865486830, 0.7071067811865464625, 0.000000000000000000 ) ) ;
#87110=ORIENTED_EDGE ( 'NONE', *, *, #67631, .T. ) ;
#87112=ORIENTED_EDGE ( 'NONE', *, *, #44175, .F. ) ;
#87113=VERTEX_POINT ( 'NONE', #129959 ) ;
#87114=PLANE ( 'NONE',  #855 ) ;
#87115=VECTOR ( 'NONE', #16832, 1000.000000000000000 ) ;
#87116=ORIENTED_EDGE ( 'NONE', *, *, #102202, .T. ) ;
#87117=VECTOR ( 'NONE', #95981, 1000.000000000000227 ) ;
#87119=ORIENTED_EDGE ( 'NONE', *, *, #18103, .F. ) ;
#87120=DIRECTION ( 'NONE',  ( -0.7071067811865486830, 0.7071067811865464625, 0.000000000000000000 ) ) ;
#87121=VERTEX_POINT ( 'NONE', #142963 ) ;
#87122=DIRECTION ( 'NONE',  ( 0.7071067811865487940, -0.7071067811865463515, 0.000000000000000000 ) ) ;
#87123=FACE_OUTER_BOUND ( 'NONE', #42267, .T. ) ;
#87124=ORIENTED_EDGE ( 'NONE', *, *, #61898, .T. ) ;
#87125=CARTESIAN_POINT ( 'NONE',  ( 34.92499999999998295, -4.199905483972782072, 4.759050581649323597 ) ) ;
#87126=CARTESIAN_POINT ( 'NONE',  ( 31.49999999999977973, -5.947814304570761657, 5.000000000000000000 ) ) ;
#87128=EDGE_CURVE ( 'NONE', #40303, #20803, #74150, .T. ) ;
#87130=FACE_OUTER_BOUND ( 'NONE', #86867, .T. ) ;
#87132=LINE ( 'NONE', #55220, #55145 ) ;
#87133=CARTESIAN_POINT ( 'NONE',  ( -2.994519915287485734, 28.92564299267940342, 4.000000000000000000 ) ) ;
#87134=CARTESIAN_POINT ( 'NONE',  ( -39.29974487139159578, -27.71228299555233576, 4.000000000000000000 ) ) ;
#87135=ORIENTED_EDGE ( 'NONE', *, *, #103162, .F. ) ;
#87137=ORIENTED_EDGE ( 'NONE', *, *, #59410, .T. ) ;
#87139=DIRECTION ( 'NONE',  ( -0.6830127018922181881, 0.6830127018922202975, -0.2588190451025214056 ) ) ;
#87141=ORIENTED_EDGE ( 'NONE', *, *, #18502, .T. ) ;
#87142=DIRECTION ( 'NONE',  ( -0.000000000000000000, 0.000000000000000000, 1.000000000000000000 ) ) ;
#87143=CARTESIAN_POINT ( 'NONE',  ( -5.700255128608413102, -27.71228299555201957, 4.000000000000000000 ) ) ;
#87144=ADVANCED_FACE ( 'NONE', ( #32069 ), #140806, .T. ) ;
#87145=PLANE ( 'NONE',  #76230 ) ;
#87147=CARTESIAN_POINT ( 'NONE',  ( -42.48921356237308800, -27.52281430457085065, 5.000000000000000000 ) ) ;
#87148=CARTESIAN_POINT ( 'NONE',  ( 3.836528711265472236, 15.75929247661555443, 9.299976744542929552 ) ) ;
#87150=DIRECTION ( 'NONE',  ( -0.7071067811865486830, -0.7071067811865464625, -0.000000000000000000 ) ) ;
#87151=ORIENTED_EDGE ( 'NONE', *, *, #72562, .T. ) ;
#87153=PLANE ( 'NONE',  #35066 ) ;
#87154=CARTESIAN_POINT ( 'NONE',  ( 21.29974487139158512, -27.71228299555221142, 4.000000000000000000 ) ) ;
#87155=CARTESIAN_POINT ( 'NONE',  ( -2.207106781186519928, -20.24070752338407075, 5.000000000000000000 ) ) ;
#87156=ORIENTED_EDGE ( 'NONE', *, *, #129200, .T. ) ;
#87157=AXIS2_PLACEMENT_3D ( 'NONE', #116466, #47684, #36071 ) ;
#87158=PLANE ( 'NONE',  #50882 ) ;
#87159=EDGE_LOOP ( 'NONE', ( #46603, #46220, #131409, #24819 ) ) ;
#87160=CARTESIAN_POINT ( 'NONE',  ( -2.510786437626908008, -27.52281430457053446, 5.000000000000000000 ) ) ;
#87161=DIRECTION ( 'NONE',  ( 0.7071067811865487940, -0.7071067811865463515, 0.000000000000000000 ) ) ;
#87162=CARTESIAN_POINT ( 'NONE',  ( -45.18398860626900415, 28.73617430169818832, 5.000000000000000000 ) ) ;
#87163=ORIENTED_EDGE ( 'NONE', *, *, #11279, .T. ) ;
#87164=CARTESIAN_POINT ( 'NONE',  ( 14.99999999999990230, -22.22500000000000142, 4.412002311790040210 ) ) ;
#87165=FACE_OUTER_BOUND ( 'NONE', #2548, .T. ) ;
#87166=EDGE_CURVE ( 'NONE', #105009, #46120, #19757, .T. ) ;
#87167=VECTOR ( 'NONE', #43882, 999.9999999999998863 ) ;
#87168=VERTEX_POINT ( 'NONE', #41504 ) ;
#87170=CARTESIAN_POINT ( 'NONE',  ( 12.00548008471251293, 28.92564299267929684, 4.000000000000000000 ) ) ;
#87172=CARTESIAN_POINT ( 'NONE',  ( -22.82816939922336985, -8.240707523384202204, 4.000000000000000000 ) ) ;
#87173=DIRECTION ( 'NONE',  ( 1.000000000000000000, 0.000000000000000000, 0.000000000000000000 ) ) ;
#87174=EDGE_LOOP ( 'NONE', ( #65369, #41690, #84042, #130777 ) ) ;
#87175=EDGE_CURVE ( 'NONE', #63012, #11599, #86466, .T. ) ;
#87176=ORIENTED_EDGE ( 'NONE', *, *, #127901, .F. ) ;
#87177=DIRECTION ( 'NONE',  ( 0.3543493200069162685, -0.000000000000000000, -0.9351131265310288487 ) ) ;
#87179=ORIENTED_EDGE ( 'NONE', *, *, #25151, .F. ) ;
#87180=VECTOR ( 'NONE', #86604, 1000.000000000000000 ) ;
#87182=EDGE_CURVE ( 'NONE', #125316, #137586, #95888, .T. ) ;
#87183=EDGE_CURVE ( 'NONE', #19965, #71257, #98046, .T. ) ;
#87185=DIRECTION ( 'NONE',  ( 0.7071067811865487940, 0.7071067811865463515, -0.000000000000000000 ) ) ;
#87186=ADVANCED_FACE ( 'NONE', ( #106749 ), #130694, .F. ) ;
#87188=ORIENTED_EDGE ( 'NONE', *, *, #139126, .T. ) ;
#87189=PLANE ( 'NONE',  #4902 ) ;
#87190=EDGE_CURVE ( 'NONE', #121898, #71767, #75586, .T. ) ;
#87191=PLANE ( 'NONE',  #72182 ) ;
#87193=EDGE_CURVE ( 'NONE', #93762, #67859, #64705, .T. ) ;
#87195=CARTESIAN_POINT ( 'NONE',  ( 0.000000000000000000, 0.000000000000000000, 5.000000000000000000 ) ) ;
#87196=ORIENTED_EDGE ( 'NONE', *, *, #121105, .T. ) ;
#87198=CARTESIAN_POINT ( 'NONE',  ( 29.20710678118634007, 6.759292476615651246, 5.000000000000000000 ) ) ;
#87200=ORIENTED_EDGE ( 'NONE', *, *, #105336, .F. ) ;
#87202=EDGE_LOOP ( 'NONE', ( #6200, #31190, #9472, #23683 ) ) ;
#87203=CARTESIAN_POINT ( 'NONE',  ( -1.171830600776461173, -17.24070752338411339, 4.000000000000000000 ) ) ;
#87204=PLANE ( 'NONE',  #97212 ) ;
#87205=ORIENTED_EDGE ( 'NONE', *, *, #112393, .T. ) ;
#87207=CARTESIAN_POINT ( 'NONE',  ( 69.48921356237309510, -27.52281430457103895, 5.000000000000000000 ) ) ;
#87208=ADVANCED_FACE ( 'NONE', ( #78437 ), #55992, .F. ) ;
#87209=FACE_OUTER_BOUND ( 'NONE', #82233, .T. ) ;
#87210=VECTOR ( 'NONE', #80155, 1000.000000000000000 ) ;
#87211=EDGE_CURVE ( 'NONE', #134939, #99796, #44407, .T. ) ;
#87212=CARTESIAN_POINT ( 'NONE',  ( -24.99033360189226372, 3.759292476615678336, 4.478963035907990609 ) ) ;
#87214=ORIENTED_EDGE ( 'NONE', *, *, #95070, .T. ) ;
#87215=LINE ( 'NONE', #74938, #99736 ) ;
#87216=CARTESIAN_POINT ( 'NONE',  ( 22.49999999999984723, 19.39370406404969316, 1.459788787078151406 ) ) ;
#87218=CARTESIAN_POINT ( 'NONE',  ( 26.99999999999980105, 5.587461875839197845, 4.000000000000000000 ) ) ;
#87220=AXIS2_PLACEMENT_3D ( 'NONE', #83162, #137554, #126641 ) ;
#87221=CARTESIAN_POINT ( 'NONE',  ( -24.70710678118636494, -0.7407075233842718154, 5.000000000000000000 ) ) ;
#87226=LINE ( 'NONE', #8878, #141019 ) ;
#87227=ORIENTED_EDGE ( 'NONE', *, *, #72057, .T. ) ;
#87228=VERTEX_POINT ( 'NONE', #132840 ) ;
#87230=DIRECTION ( 'NONE',  ( 0.3543493200069162685, -0.000000000000000000, -0.9351131265310288487 ) ) ;
#87231=DIRECTION ( 'NONE',  ( -0.6830127018922180770, -0.6830127018922204085, -0.2588190451025213501 ) ) ;
#87232=VECTOR ( 'NONE', #54959, 1000.000000000000000 ) ;
#87234=EDGE_LOOP ( 'NONE', ( #32374, #73913, #27736, #14916 ) ) ;
#87236=DIRECTION ( 'NONE',  ( -0.000000000000000000, 0.3543493200069153248, 0.9351131265310292928 ) ) ;
#87238=ORIENTED_EDGE ( 'NONE', *, *, #83240, .F. ) ;
#87239=ADVANCED_FACE ( 'NONE', ( #68312 ), #34942, .F. ) ;
#87241=ORIENTED_EDGE ( 'NONE', *, *, #88249, .F. ) ;
#87242=ORIENTED_EDGE ( 'NONE', *, *, #34673, .T. ) ;
#87243=CARTESIAN_POINT ( 'NONE',  ( 21.83652871126535899, 15.75929247661555443, 9.299976744542970408 ) ) ;
#87245=DIRECTION ( 'NONE',  ( -0.7071067811865487940, 0.7071067811865463515, 0.000000000000000000 ) ) ;
#87246=DIRECTION ( 'NONE',  ( -0.7071067811865487940, 0.7071067811865463515, 0.000000000000000000 ) ) ;
#87247=ORIENTED_EDGE ( 'NONE', *, *, #7135, .F. ) ;
#87248=FACE_OUTER_BOUND ( 'NONE', #92461, .T. ) ;
#87249=DIRECTION ( 'NONE',  ( -0.7071067811865486830, -0.7071067811865464625, -0.000000000000000000 ) ) ;
#87250=CARTESIAN_POINT ( 'NONE',  ( 2.671830600776449405, -3.740707523384248390, 4.000000000000000000 ) ) ;
#87253=CARTESIAN_POINT ( 'NONE',  ( -6.874853806907617049, -14.24070752338413648, 9.401115078912674505 ) ) ;
#87256=CARTESIAN_POINT ( 'NONE',  ( -66.18398860626901126, 28.73617430169833753, 5.000000000000000000 ) ) ;
#87257=EDGE_CURVE ( 'NONE', #130662, #43690, #66147, .T. ) ;
#87258=ORIENTED_EDGE ( 'NONE', *, *, #85485, .F. ) ;
#87260=DIRECTION ( 'NONE',  ( -0.000000000000000000, -0.000000000000000000, 1.000000000000000000 ) ) ;
#87262=CARTESIAN_POINT ( 'NONE',  ( 17.51078643762690845, -27.52281430457043143, 5.000000000000000000 ) ) ;
#87263=EDGE_CURVE ( 'NONE', #127403, #130838, #23304, .T. ) ;
#87264=LINE ( 'NONE', #43757, #119569 ) ;
#87265=DIRECTION ( 'NONE',  ( -0.6830127018922181881, 0.6830127018922202975, -0.2588190451025214056 ) ) ;
#87266=ORIENTED_EDGE ( 'NONE', *, *, #42185, .T. ) ;
#87267=ORIENTED_EDGE ( 'NONE', *, *, #99306, .F. ) ;
#87269=CARTESIAN_POINT ( 'NONE',  ( -18.18398860626898994, 28.73617430169800002, 5.000000000000000000 ) ) ;
#87270=CARTESIAN_POINT ( 'NONE',  ( -15.67180000000000639, 3.174999999999997158, 0.000000000000000000 ) ) ;
#87271=EDGE_LOOP ( 'NONE', ( #137144, #72639, #10460, #107000 ) ) ;
#87272=( BOUNDED_CURVE ( )  B_SPLINE_CURVE ( 3, ( #6781, #95260, #139530, #84420 ),
 .UNSPECIFIED., .F., .F. ) 
 B_SPLINE_CURVE_WITH_KNOTS ( ( 4, 4 ),
 ( 2.001653308786157659, 3.503810798801451742 ),
 .UNSPECIFIED. ) 
 CURVE ( )  GEOMETRIC_REPRESENTATION_ITEM ( )  RATIONAL_B_SPLINE_CURVE ( ( 1.000000000000000000, 0.8206354192515212809, 0.8206354192515212809, 1.000000000000000000 ) ) 
 REPRESENTATION_ITEM ( '' )  );
#87273=EDGE_LOOP ( 'NONE', ( #137209, #53326, #128216, #13288 ) ) ;
#87274=EDGE_CURVE ( 'NONE', #59884, #130856, #2994, .T. ) ;
#87275=DIRECTION ( 'NONE',  ( -0.7071067811865487940, 0.7071067811865463515, -0.000000000000000000 ) ) ;
#87276=ORIENTED_EDGE ( 'NONE', *, *, #124819, .F. ) ;
#87278=CARTESIAN_POINT ( 'NONE',  ( 12.79289321881336861, 0.7592924766157086447, 5.000000000000000000 ) ) ;
#87279=VECTOR ( 'NONE', #42128, 1000.000000000000000 ) ;
#87280=( BOUNDED_CURVE ( )  B_SPLINE_CURVE ( 3, ( #37710, #26806, #15883, #60172 ),
 .UNSPECIFIED., .F., .F. ) 
 B_SPLINE_CURVE_WITH_KNOTS ( ( 4, 4 ),
 ( 4.257860004652494368, 4.307247239014357021 ),
 .UNSPECIFIED. ) 
 CURVE ( )  GEOMETRIC_REPRESENTATION_ITEM ( )  RATIONAL_B_SPLINE_CURVE ( ( 1.000000000000000000, 0.9997967520851089862, 0.9997967520851089862, 1.000000000000000000 ) ) 
 REPRESENTATION_ITEM ( '' )  );
#87281=FACE_OUTER_BOUND ( 'NONE', #76306, .T. ) ;
#87282=VECTOR ( 'NONE', #22346, 1000.000000000000000 ) ;
#87283=EDGE_CURVE ( 'NONE', #44324, #109623, #90000, .T. ) ;
#87284=FACE_BOUND ( 'NONE', #35163, .T. ) ;
#87285=LINE ( 'NONE', #73557, #45619 ) ;
#87286=CARTESIAN_POINT ( 'NONE',  ( -53.99451991528749062, 28.92564299267975869, 4.000000000000000000 ) ) ;
#87287=CARTESIAN_POINT ( 'NONE',  ( -11.93988928955972639, -9.740707523384184441, 10.89222023123383565 ) ) ;
#87288=DIRECTION ( 'NONE',  ( -0.7071067811865486830, 0.7071067811865464625, 0.000000000000000000 ) ) ;
#87289=ORIENTED_EDGE ( 'NONE', *, *, #87684, .T. ) ;
#87290=DIRECTION ( 'NONE',  ( -0.7071067811865487940, 0.7071067811865463515, -0.000000000000000000 ) ) ;
#87292=ORIENTED_EDGE ( 'NONE', *, *, #6728, .F. ) ;
#87293=ORIENTED_EDGE ( 'NONE', *, *, #19322, .F. ) ;
#87295=ORIENTED_EDGE ( 'NONE', *, *, #22055, .F. ) ;
#87296=DIRECTION ( 'NONE',  ( -0.7071067811865487940, 0.7071067811865463515, -0.000000000000000000 ) ) ;
#87297=VECTOR ( 'NONE', #94566, 1000.000000000000227 ) ;
#87298=LINE ( 'NONE', #30789, #139285 ) ;
#87299=ORIENTED_EDGE ( 'NONE', *, *, #67268, .F. ) ;
#87302=CARTESIAN_POINT ( 'NONE',  ( 34.92499999999998295, 12.00612307739183571, 4.000000000000000000 ) ) ;
#87303=DIRECTION ( 'NONE',  ( -0.6830127018922181881, 0.6830127018922202975, -0.2588190451025214056 ) ) ;
#87304=EDGE_CURVE ( 'NONE', #98171, #482, #10989, .T. ) ;
#87305=PLANE ( 'NONE',  #110231 ) ;
#87306=LINE ( 'NONE', #32212, #27345 ) ;
#87307=DIRECTION ( 'NONE',  ( 0.7071067811865487940, -0.7071067811865463515, 0.000000000000000000 ) ) ;
#87308=CARTESIAN_POINT ( 'NONE',  ( 4.499999999999968914, -16.91253812416058722, 4.000000000000000000 ) ) ;
#87309=CARTESIAN_POINT ( 'NONE',  ( -30.48921356237309510, -27.52281430457076894, 5.000000000000000000 ) ) ;
#87310=ORIENTED_EDGE ( 'NONE', *, *, #21404, .T. ) ;
#87311=DIRECTION ( 'NONE',  ( 0.7071067811865487940, 0.7071067811865463515, -0.000000000000000000 ) ) ;
#87312=ORIENTED_EDGE ( 'NONE', *, *, #130232, .T. ) ;
#87313=DIRECTION ( 'NONE',  ( 0.7071067811865486830, -0.7071067811865464625, -0.000000000000000000 ) ) ;
#87314=CARTESIAN_POINT ( 'NONE',  ( 36.29974487139159578, -27.71228299555231445, 4.000000000000000000 ) ) ;
#87315=ORIENTED_EDGE ( 'NONE', *, *, #53172, .F. ) ;
#87316=VECTOR ( 'NONE', #84769, 1000.000000000000000 ) ;
#87317=ORIENTED_EDGE ( 'NONE', *, *, #28333, .T. ) ;
#87318=EDGE_CURVE ( 'NONE', #133992, #23088, #122633, .T. ) ;
#87320=ORIENTED_EDGE ( 'NONE', *, *, #109756, .F. ) ;
#87321=DIRECTION ( 'NONE',  ( 0.3543493200069163795, -9.265275131829747941E-33, -0.9351131265310288487 ) ) ;
#87324=VECTOR ( 'NONE', #128645, 1000.000000000000000 ) ;
#87325=LINE ( 'NONE', #45279, #37731 ) ;
#87326=AXIS2_PLACEMENT_3D ( 'NONE', #55888, #109526, #76195 ) ;
#87329=ORIENTED_EDGE ( 'NONE', *, *, #44624, .F. ) ;
#87331=VECTOR ( 'NONE', #35329, 1000.000000000000000 ) ;
#87332=ORIENTED_EDGE ( 'NONE', *, *, #50931, .F. ) ;
#87335=CARTESIAN_POINT ( 'NONE',  ( -66.18398860626901126, 28.73617430169833753, 5.000000000000000000 ) ) ;
#87336=FACE_OUTER_BOUND ( 'NONE', #4846, .T. ) ;
#87337=ORIENTED_EDGE ( 'NONE', *, *, #135121, .T. ) ;
#87338=ORIENTED_EDGE ( 'NONE', *, *, #18086, .F. ) ;
#87339=CARTESIAN_POINT ( 'NONE',  ( -21.29974487139158512, -27.71228299555221142, 4.000000000000000000 ) ) ;
#87341=DIRECTION ( 'NONE',  ( 0.7071067811865486830, -0.7071067811865464625, -0.000000000000000000 ) ) ;
#87342=ORIENTED_EDGE ( 'NONE', *, *, #2969, .F. ) ;
#87343=CARTESIAN_POINT ( 'NONE',  ( -39.48921356237310221, -27.52281430457082934, 5.000000000000000000 ) ) ;
#87346=ORIENTED_EDGE ( 'NONE', *, *, #73257, .T. ) ;
#87347=CARTESIAN_POINT ( 'NONE',  ( 32.99999999999976552, 10.21212019023812623, -2.019456568337874458 ) ) ;
#87348=CARTESIAN_POINT ( 'NONE',  ( 8.292893218813398803, -15.74070752338412049, 5.000000000000000000 ) ) ;
#87349=CARTESIAN_POINT ( 'NONE',  ( -19.05000000000000071, 3.174999999999997158, 5.000000000000000000 ) ) ;
#87350=CARTESIAN_POINT ( 'NONE',  ( -57.18398860626899705, 28.73617430169827358, 5.000000000000000000 ) ) ;
#87351=CARTESIAN_POINT ( 'NONE',  ( -57.18398860626899705, 28.73617430169827358, 5.000000000000000000 ) ) ;
#87352=DIRECTION ( 'NONE',  ( 0.7071067811865487940, 0.7071067811865463515, 0.000000000000000000 ) ) ;
#87353=CARTESIAN_POINT ( 'NONE',  ( -34.92500000000001137, 19.70193056682081334, 4.500000000000000888 ) ) ;
#87354=ORIENTED_EDGE ( 'NONE', *, *, #18444, .T. ) ;
#87357=AXIS2_PLACEMENT_3D ( 'NONE', #68978, #12420, #133509 ) ;
#87358=CARTESIAN_POINT ( 'NONE',  ( -5.510786437626906675, -27.52281430457051314, 5.000000000000000000 ) ) ;
#87359=DIRECTION ( 'NONE',  ( -0.7071067811865486830, -0.7071067811865464625, -0.000000000000000000 ) ) ;
#87361=VECTOR ( 'NONE', #7068, 1000.000000000000000 ) ;
#87363=CARTESIAN_POINT ( 'NONE',  ( 21.18398860626899349, 28.73617430169802134, 5.000000000000000000 ) ) ;
#87364=DIRECTION ( 'NONE',  ( 0.7071067811865487940, 0.7071067811865463515, -0.000000000000000000 ) ) ;
#87365=PLANE ( 'NONE',  #28195 ) ;
#87366=VERTEX_POINT ( 'NONE', #33528 ) ;
#87367=EDGE_CURVE ( 'NONE', #63264, #124966, #34218, .T. ) ;
#87368=EDGE_LOOP ( 'NONE', ( #85465, #141137, #38396, #16636 ) ) ;
#87370=DIRECTION ( 'NONE',  ( 0.7071067811865487940, 0.7071067811865463515, 0.000000000000000000 ) ) ;
#87373=CARTESIAN_POINT ( 'NONE',  ( 11.29289321881338282, 11.25929247661560773, 5.000000000000000000 ) ) ;
#87374=CARTESIAN_POINT ( 'NONE',  ( -60.18398860626900415, 28.73617430169829490, 5.000000000000000000 ) ) ;
#87375=EDGE_CURVE ( 'NONE', #22559, #122500, #125513, .T. ) ;
#87377=DIRECTION ( 'NONE',  ( -1.000000000000000000, 0.000000000000000000, -0.000000000000000000 ) ) ;
#87378=DIRECTION ( 'NONE',  ( -0.000000000000000000, -0.3543493200069152693, 0.9351131265310292928 ) ) ;
#87379=CARTESIAN_POINT ( 'NONE',  ( 27.18398860626900060, 28.73617430169806042, 5.000000000000000000 ) ) ;
#87380=CARTESIAN_POINT ( 'NONE',  ( 22.49999999999984368, -20.53675388469228480, 2.352720554255944840 ) ) ;
#87381=ORIENTED_EDGE ( 'NONE', *, *, #102065, .T. ) ;
#87384=VERTEX_POINT ( 'NONE', #94288 ) ;
#87385=CARTESIAN_POINT ( 'NONE',  ( 17.99999999999987566, -2.904428200921286951, -6.989807076074982639 ) ) ;
#87386=DIRECTION ( 'NONE',  ( -0.3543493200069162685, -0.000000000000000000, -0.9351131265310288487 ) ) ;
#87387=ORIENTED_EDGE ( 'NONE', *, *, #115981, .T. ) ;
#87388=CARTESIAN_POINT ( 'NONE',  ( -45.18398860626900415, 28.73617430169818832, 5.000000000000000000 ) ) ;
#87389=DIRECTION ( 'NONE',  ( -0.7071067811865486830, -0.7071067811865464625, 0.000000000000000000 ) ) ;
#87392=LINE ( 'NONE', #23547, #92502 ) ;
#87393=AXIS2_PLACEMENT_3D ( 'NONE', #104931, #94051, #127393 ) ;
#87394=EDGE_CURVE ( 'NONE', #93361, #927, #15979, .T. ) ;
#87395=CARTESIAN_POINT ( 'NONE',  ( -9.516654386410381861, 22.22500000000000142, 4.500000000000000888 ) ) ;
#87396=CARTESIAN_POINT ( 'NONE',  ( -48.48921356237309510, -27.52281430457089328, 5.000000000000000000 ) ) ;
#87398=VERTEX_POINT ( 'NONE', #39212 ) ;
#87399=LINE ( 'NONE', #66364, #28140 ) ;
#87400=DIRECTION ( 'NONE',  ( 0.7071067811865487940, -0.7071067811865463515, 0.000000000000000000 ) ) ;
#87402=EDGE_CURVE ( 'NONE', #123992, #62221, #71862, .T. ) ;
#87405=DIRECTION ( 'NONE',  ( -0.3543493200069162685, -0.000000000000000000, -0.9351131265310288487 ) ) ;
#87406=CARTESIAN_POINT ( 'NONE',  ( -30.70710678118633297, 20.25929247661551713, 5.000000000000000000 ) ) ;
#87407=EDGE_LOOP ( 'NONE', ( #53603, #19688, #73274, #91611 ) ) ;
#87408=AXIS2_PLACEMENT_3D ( 'NONE', #23246, #46509, #67523 ) ;
#87412=DIRECTION ( 'NONE',  ( 0.7071067811865487940, 0.7071067811865463515, -0.000000000000000000 ) ) ;
#87413=EDGE_CURVE ( 'NONE', #142592, #90987, #126218, .T. ) ;
#87414=VERTEX_POINT ( 'NONE', #137094 ) ;
#87415=CARTESIAN_POINT ( 'NONE',  ( 39.48921356237310221, -27.52281430457082934, 5.000000000000000000 ) ) ;
#87417=AXIS2_PLACEMENT_3D ( 'NONE', #117664, #18350, #74208 ) ;
#87419=CARTESIAN_POINT ( 'NONE',  ( 75.18398860626899705, 28.73617430169839793, 5.000000000000000000 ) ) ;
#87421=ORIENTED_EDGE ( 'NONE', *, *, #45790, .F. ) ;
#87422=CARTESIAN_POINT ( 'NONE',  ( 34.92499999999998295, -2.337538124160962738, 4.000000000000000000 ) ) ;
#87424=CARTESIAN_POINT ( 'NONE',  ( -34.92500000000001137, -22.22500000000000142, 4.000000000000000000 ) ) ;
#87425=DIRECTION ( 'NONE',  ( -0.7071067811865486830, -0.7071067811865464625, 0.000000000000000000 ) ) ;
#87426=VECTOR ( 'NONE', #67889, 1000.000000000000000 ) ;
#87427=CARTESIAN_POINT ( 'NONE',  ( -27.48921356237309155, -27.52281430457074762, 5.000000000000000000 ) ) ;
#87429=PLANE ( 'NONE',  #5806 ) ;
#87433=DIRECTION ( 'NONE',  ( 0.7071067811865487940, -0.7071067811865463515, 0.000000000000000000 ) ) ;
#87435=VECTOR ( 'NONE', #9414, 1000.000000000000000 ) ;
#87436=FACE_OUTER_BOUND ( 'NONE', #27775, .T. ) ;
#87439=EDGE_CURVE ( 'NONE', #119594, #13220, #51525, .T. ) ;
#87440=VERTEX_POINT ( 'NONE', #119587 ) ;
#87441=VECTOR ( 'NONE', #140541, 1000.000000000000000 ) ;
#87443=ORIENTED_EDGE ( 'NONE', *, *, #112350, .T. ) ;
#87444=DIRECTION ( 'NONE',  ( -1.000000000000000000, 0.000000000000000000, 0.000000000000000000 ) ) ;
#87445=PLANE ( 'NONE',  #10952 ) ;
#87446=DIRECTION ( 'NONE',  ( 0.7071067811865486830, -0.7071067811865464625, -0.000000000000000000 ) ) ;
#87449=VERTEX_POINT ( 'NONE', #73979 ) ;
#87450=EDGE_LOOP ( 'NONE', ( #113002, #134496, #38593, #103307 ) ) ;
#87451=FACE_OUTER_BOUND ( 'NONE', #70000, .T. ) ;
#87452=CARTESIAN_POINT ( 'NONE',  ( -48.29974487139158867, -27.71228299555239971, 4.000000000000000000 ) ) ;
#87453=EDGE_LOOP ( 'NONE', ( #116714, #93576, #97516, #27638 ) ) ;
#87454=EDGE_CURVE ( 'NONE', #133840, #67716, #40646, .T. ) ;
#87455=CARTESIAN_POINT ( 'NONE',  ( -29.91685193227051087, 21.75929247661549581, 7.311836541447982007 ) ) ;
#87457=DIRECTION ( 'NONE',  ( -0.7071067811865486830, -0.7071067811865464625, 0.000000000000000000 ) ) ;
#87458=VERTEX_POINT ( 'NONE', #118896 ) ;
#87459=EDGE_CURVE ( 'NONE', #65140, #113212, #141368, .T. ) ;
#87460=CARTESIAN_POINT ( 'NONE',  ( 54.18398860626899705, 28.73617430169825226, 5.000000000000000000 ) ) ;
#87462=DIRECTION ( 'NONE',  ( -0.000000000000000000, -0.3543493200069152693, 0.9351131265310292928 ) ) ;
#87463=DIRECTION ( 'NONE',  ( -0.000000000000000000, 0.000000000000000000, 1.000000000000000000 ) ) ;
#87464=VECTOR ( 'NONE', #123697, 1000.000000000000000 ) ;
#87467=FACE_OUTER_BOUND ( 'NONE', #89609, .T. ) ;
#87468=ORIENTED_EDGE ( 'NONE', *, *, #58486, .F. ) ;
#87469=ORIENTED_EDGE ( 'NONE', *, *, #111575, .T. ) ;
#87471=ORIENTED_EDGE ( 'NONE', *, *, #46477, .F. ) ;
#87472=ORIENTED_EDGE ( 'NONE', *, *, #137953, .F. ) ;
#87475=CARTESIAN_POINT ( 'NONE',  ( 3.005480084712505828, 28.92564299267936079, 4.000000000000000000 ) ) ;
#87476=EDGE_LOOP ( 'NONE', ( #61734, #55925, #112309, #89918 ) ) ;
#87477=LINE ( 'NONE', #52685, #133973 ) ;
#87478=DIRECTION ( 'NONE',  ( -0.000000000000000000, 0.3543493200069153248, 0.9351131265310292928 ) ) ;
#87479=EDGE_CURVE ( 'NONE', #86941, #92661, #86294, .T. ) ;
#87480=FACE_OUTER_BOUND ( 'NONE', #67946, .T. ) ;
#87481=PLANE ( 'NONE',  #99371 ) ;
#87482=DIRECTION ( 'NONE',  ( 0.7071067811865487940, 0.7071067811865463515, 0.000000000000000000 ) ) ;
#87483=ORIENTED_EDGE ( 'NONE', *, *, #35728, .T. ) ;
#87484=CARTESIAN_POINT ( 'NONE',  ( 32.99999999999977263, 16.93112307739201228, 4.000000000000000000 ) ) ;
#87485=CARTESIAN_POINT ( 'NONE',  ( 65.99451991528749772, 28.92564299267984396, 4.000000000000000000 ) ) ;
#87487=EDGE_CURVE ( 'NONE', #114269, #27583, #140642, .T. ) ;
#87488=ORIENTED_EDGE ( 'NONE', *, *, #21551, .F. ) ;
#87489=EDGE_CURVE ( 'NONE', #962, #45746, #7976, .T. ) ;
#87490=ORIENTED_EDGE ( 'NONE', *, *, #106144, .F. ) ;
#87492=EDGE_LOOP ( 'NONE', ( #141138, #87870, #34250, #94658 ) ) ;
#87494=CARTESIAN_POINT ( 'NONE',  ( -63.18398860626900415, 28.73617430169831621, 5.000000000000000000 ) ) ;
#87495=VECTOR ( 'NONE', #92080, 1000.000000000000000 ) ;
#87497=CARTESIAN_POINT ( 'NONE',  ( 11.67183060077639212, -6.740707523384212863, 4.000000000000000000 ) ) ;
#87498=LINE ( 'NONE', #53432, #109070 ) ;
#87499=ORIENTED_EDGE ( 'NONE', *, *, #85453, .F. ) ;
#87501=DIRECTION ( 'NONE',  ( 0.7071067811865487940, 0.7071067811865463515, -0.000000000000000000 ) ) ;
#87502=ADVANCED_FACE ( 'NONE', ( #10136 ), #73281, .F. ) ;
#87503=CARTESIAN_POINT ( 'NONE',  ( 34.49999999999975131, -14.70932175296474398, -11.46312253303845274 ) ) ;
#87504=DIRECTION ( 'NONE',  ( -0.7071067811865486830, -0.7071067811865464625, -0.000000000000000000 ) ) ;
#87507=LINE ( 'NONE', #53442, #13602 ) ;
#87509=ORIENTED_EDGE ( 'NONE', *, *, #45082, .F. ) ;
#87510=ORIENTED_EDGE ( 'NONE', *, *, #142037, .F. ) ;
#87512=EDGE_LOOP ( 'NONE', ( #43283, #57782, #101631, #1590 ) ) ;
#87513=VECTOR ( 'NONE', #16329, 1000.000000000000000 ) ;
#87514=DIRECTION ( 'NONE',  ( -0.7071067811865486830, -0.7071067811865464625, 0.000000000000000000 ) ) ;
#87515=VECTOR ( 'NONE', #83565, 1000.000000000000000 ) ;
#87516=FACE_OUTER_BOUND ( 'NONE', #15244, .T. ) ;
#87518=CARTESIAN_POINT ( 'NONE',  ( 10.98012225071445869, -17.24070752338409918, 20.23474786156471694 ) ) ;
#87519=ORIENTED_EDGE ( 'NONE', *, *, #78858, .F. ) ;
#87520=VECTOR ( 'NONE', #41115, 1000.000000000000000 ) ;
#87521=VECTOR ( 'NONE', #102110, 1000.000000000000000 ) ;
#87523=EDGE_CURVE ( 'NONE', #141614, #18270, #64523, .T. ) ;
#87524=CARTESIAN_POINT ( 'NONE',  ( -8.999999999999937828, 9.631307414974314085, -9.079085613539563226 ) ) ;
#87527=EDGE_CURVE ( 'NONE', #14243, #135923, #52900, .T. ) ;
#87528=ORIENTED_EDGE ( 'NONE', *, *, #26830, .T. ) ;
#87529=ORIENTED_EDGE ( 'NONE', *, *, #17027, .T. ) ;
#87530=FACE_OUTER_BOUND ( 'NONE', #21023, .T. ) ;
#87532=PLANE ( 'NONE',  #31133 ) ;
#87533=CARTESIAN_POINT ( 'NONE',  ( 30.29974487139158867, -27.71228299555227537, 4.000000000000000000 ) ) ;
#87534=EDGE_CURVE ( 'NONE', #89571, #37298, #108701, .T. ) ;
#87535=EDGE_CURVE ( 'NONE', #140583, #125898, #97871, .T. ) ;
#87536=CARTESIAN_POINT ( 'NONE',  ( 29.99999999999981171, -19.44781430457063465, 5.000000000000000000 ) ) ;
#87538=DIRECTION ( 'NONE',  ( 0.7071067811865487940, 0.7071067811865463515, -0.000000000000000000 ) ) ;
#87539=CARTESIAN_POINT ( 'NONE',  ( -34.92500000000001847, -1.487538124160473707, 4.000000000000000000 ) ) ;
#87543=PLANE ( 'NONE',  #15184 ) ;
#87544=ORIENTED_EDGE ( 'NONE', *, *, #5384, .F. ) ;
#87545=VECTOR ( 'NONE', #127856, 1000.000000000000000 ) ;
#87547=PLANE ( 'NONE',  #37205 ) ;
#87548=ORIENTED_EDGE ( 'NONE', *, *, #91387, .F. ) ;
#87549=ADVANCED_FACE ( 'NONE', ( #9386 ), #53666, .F. ) ;
#87550=ADVANCED_FACE ( 'NONE', ( #21005 ), #109453, .T. ) ;
#87551=CARTESIAN_POINT ( 'NONE',  ( 17.99999999999988987, 14.58746187583909126, 4.000000000000000000 ) ) ;
#87552=EDGE_LOOP ( 'NONE', ( #37811, #31297, #139776, #72876 ) ) ;
#87553=CARTESIAN_POINT ( 'NONE',  ( -23.99451991528749062, 28.92564299267954908, 4.000000000000000000 ) ) ;
#87554=VECTOR ( 'NONE', #76079, 1000.000000000000227 ) ;
#87555=ORIENTED_EDGE ( 'NONE', *, *, #50001, .F. ) ;
#87556=DIRECTION ( 'NONE',  ( -0.6830127018922181881, 0.6830127018922202975, -0.2588190451025214056 ) ) ;
#87557=ORIENTED_EDGE ( 'NONE', *, *, #26978, .F. ) ;
#87560=PLANE ( 'NONE',  #143395 ) ;
#87561=EDGE_CURVE ( 'NONE', #39257, #68534, #142798, .T. ) ;
#87562=CARTESIAN_POINT ( 'NONE',  ( 63.48921356237309510, -27.52281430457099631, 5.000000000000000000 ) ) ;
#87563=PLANE ( 'NONE',  #72388 ) ;
#87565=CARTESIAN_POINT ( 'NONE',  ( 26.20710678118635784, 3.759292476615673007, 5.000000000000000000 ) ) ;
#87568=EDGE_CURVE ( 'NONE', #25152, #98769, #57251, .T. ) ;
#87569=VECTOR ( 'NONE', #122415, 999.9999999999998863 ) ;
#87570=DIRECTION ( 'NONE',  ( 0.7071067811865487940, 0.7071067811865463515, 0.000000000000000000 ) ) ;
#87571=CYLINDRICAL_SURFACE ( 'NONE', #24713, 0.5000000000000004441 ) ;
#87572=ORIENTED_EDGE ( 'NONE', *, *, #3165, .F. ) ;
#87573=ORIENTED_EDGE ( 'NONE', *, *, #113853, .T. ) ;
#87574=DIRECTION ( 'NONE',  ( -0.000000000000000000, 0.3543493200069152138, -0.9351131265310292928 ) ) ;
#87575=ORIENTED_EDGE ( 'NONE', *, *, #116135, .F. ) ;
#87576=CARTESIAN_POINT ( 'NONE',  ( 14.20710678118644843, 9.759292476615620160, 5.000000000000000000 ) ) ;
#87577=ADVANCED_FACE ( 'NONE', ( #67407 ), #68147, .T. ) ;
#87578=DIRECTION ( 'NONE',  ( 0.7071067811865486830, -0.7071067811865464625, -0.000000000000000000 ) ) ;
#87580=VERTEX_POINT ( 'NONE', #21740 ) ;
#87584=CARTESIAN_POINT ( 'NONE',  ( 0.7586007421979610310, 21.72500000000000853, 5.000000000000000000 ) ) ;
#87585=DIRECTION ( 'NONE',  ( 0.7071067811865486830, -0.7071067811865464625, -0.000000000000000000 ) ) ;
#87586=DIRECTION ( 'NONE',  ( 0.3543493200069163240, -0.000000000000000000, -0.9351131265310288487 ) ) ;
#87587=EDGE_CURVE ( 'NONE', #50406, #137620, #24579, .T. ) ;
#87588=VERTEX_POINT ( 'NONE', #132679 ) ;
#87589=LINE ( 'NONE', #63716, #106790 ) ;
#87590=EDGE_CURVE ( 'NONE', #48371, #55182, #110148, .T. ) ;
#87592=LINE ( 'NONE', #41956, #625 ) ;
#87594=DIRECTION ( 'NONE',  ( -0.7071067811865487940, 0.7071067811865463515, -0.000000000000000000 ) ) ;
#87595=ORIENTED_EDGE ( 'NONE', *, *, #125021, .F. ) ;
#87596=EDGE_CURVE ( 'NONE', #91253, #51436, #43488, .T. ) ;
#87597=ORIENTED_EDGE ( 'NONE', *, *, #40269, .T. ) ;
#87598=VERTEX_POINT ( 'NONE', #134075 ) ;
#87600=AXIS2_PLACEMENT_3D ( 'NONE', #10262, #95855, #53808 ) ;
#87601=ORIENTED_EDGE ( 'NONE', *, *, #20375, .F. ) ;
#87604=VERTEX_POINT ( 'NONE', #113007 ) ;
#87605=CARTESIAN_POINT ( 'NONE',  ( 14.99999999999990230, -6.108550654416941228, -3.114665004254935088 ) ) ;
#87606=CARTESIAN_POINT ( 'NONE',  ( -32.67183060077623935, 14.25929247661556865, 4.000000000000000000 ) ) ;
#87608=EDGE_LOOP ( 'NONE', ( #130299, #18759, #112212, #14926 ) ) ;
#87609=DIRECTION ( 'NONE',  ( 0.7071067811865487940, 0.7071067811865463515, -0.000000000000000000 ) ) ;
#87610=DIRECTION ( 'NONE',  ( 0.7071067811865486830, -0.7071067811865464625, -0.000000000000000000 ) ) ;
#87612=VECTOR ( 'NONE', #93044, 1000.000000000000227 ) ;
#87616=ORIENTED_EDGE ( 'NONE', *, *, #135968, .T. ) ;
#87617=DIRECTION ( 'NONE',  ( -0.7071067811865486830, -0.7071067811865464625, -0.000000000000000000 ) ) ;
#87618=VECTOR ( 'NONE', #66508, 1000.000000000000000 ) ;
#87619=DIRECTION ( 'NONE',  ( 0.7071067811865486830, -0.7071067811865464625, -0.000000000000000000 ) ) ;
#87620=LINE ( 'NONE', #99928, #32666 ) ;
#87622=AXIS2_PLACEMENT_3D ( 'NONE', #70686, #114834, #15512 ) ;
#87624=DIRECTION ( 'NONE',  ( -0.7071067811865486830, -0.7071067811865464625, 0.000000000000000000 ) ) ;
#87626=EDGE_LOOP ( 'NONE', ( #48523, #10045, #117170, #94066 ) ) ;
#87627=ORIENTED_EDGE ( 'NONE', *, *, #116405, .T. ) ;
#87628=LINE ( 'NONE', #9299, #110466 ) ;
#87629=EDGE_LOOP ( 'NONE', ( #134718, #7088, #30034, #85430 ) ) ;
#87630=EDGE_CURVE ( 'NONE', #40076, #50446, #44224, .T. ) ;
#87631=ORIENTED_EDGE ( 'NONE', *, *, #56991, .F. ) ;
#87632=VECTOR ( 'NONE', #77048, 1000.000000000000227 ) ;
#87633=VECTOR ( 'NONE', #66533, 1000.000000000000000 ) ;
#87634=CARTESIAN_POINT ( 'NONE',  ( -18.29974487139159223, -27.71228299555219010, 4.000000000000000000 ) ) ;
#87635=ORIENTED_EDGE ( 'NONE', *, *, #9960, .F. ) ;
#87636=DIRECTION ( 'NONE',  ( 0.000000000000000000, -1.000000000000000000, 0.000000000000000000 ) ) ;
#87638=DIRECTION ( 'NONE',  ( 0.7071067811865487940, -0.7071067811865463515, 0.000000000000000000 ) ) ;
#87639=PLANE ( 'NONE',  #124758 ) ;
#87640=VECTOR ( 'NONE', #55121, 1000.000000000000000 ) ;
#87641=CARTESIAN_POINT ( 'NONE',  ( -26.99451991528749417, 28.92564299267956685, 4.000000000000000000 ) ) ;
#87642=ORIENTED_EDGE ( 'NONE', *, *, #119286, .F. ) ;
#87643=AXIS2_PLACEMENT_3D ( 'NONE', #104271, #81877, #60101 ) ;
#87645=ORIENTED_EDGE ( 'NONE', *, *, #5726, .F. ) ;
#87646=ADVANCED_FACE ( 'NONE', ( #13677 ), #32630, .F. ) ;
#87647=CARTESIAN_POINT ( 'NONE',  ( -45.18398860626900415, 28.73617430169818832, 5.000000000000000000 ) ) ;
#87648=VERTEX_POINT ( 'NONE', #11534 ) ;
#87650=ORIENTED_EDGE ( 'NONE', *, *, #129057, .T. ) ;
#87651=DIRECTION ( 'NONE',  ( -0.000000000000000000, -0.3543493200069152693, 0.9351131265310292928 ) ) ;
#87652=EDGE_CURVE ( 'NONE', #48047, #93569, #57969, .T. ) ;
#87653=VERTEX_POINT ( 'NONE', #131940 ) ;
#87654=VERTEX_POINT ( 'NONE', #46387 ) ;
#87655=VECTOR ( 'NONE', #100049, 1000.000000000000000 ) ;
#87656=EDGE_LOOP ( 'NONE', ( #69519, #1114, #98809, #34560 ) ) ;
#87657=PLANE ( 'NONE',  #88264 ) ;
#87658=DIRECTION ( 'NONE',  ( 1.000000000000000000, 0.000000000000000000, 0.000000000000000000 ) ) ;
#87659=CARTESIAN_POINT ( 'NONE',  ( 19.99806943317887686, -22.22500000000000142, 4.500000000000000888 ) ) ;
#87660=CARTESIAN_POINT ( 'NONE',  ( -34.92500000000001137, 1.821246448331360179, 12.73174495308782816 ) ) ;
#87662=CARTESIAN_POINT ( 'NONE',  ( -21.75860074219781382, 21.72500000000000142, 5.000000000000000000 ) ) ;
#87664=CARTESIAN_POINT ( 'NONE',  ( -65.99451991528749772, 28.92564299267984396, 4.000000000000000000 ) ) ;
#87665=LINE ( 'NONE', #32585, #55178 ) ;
#87667=PLANE ( 'NONE',  #123346 ) ;
#87669=ADVANCED_FACE ( 'NONE', ( #23120 ), #133368, .F. ) ;
#87671=DIRECTION ( 'NONE',  ( -0.000000000000000000, -0.000000000000000000, 1.000000000000000000 ) ) ;
#87672=DIRECTION ( 'NONE',  ( -0.000000000000000000, 0.3543493200069153248, 0.9351131265310292928 ) ) ;
#87673=ORIENTED_EDGE ( 'NONE', *, *, #59254, .T. ) ;
#87674=ORIENTED_EDGE ( 'NONE', *, *, #20603, .T. ) ;
#87675=ORIENTED_EDGE ( 'NONE', *, *, #126628, .F. ) ;
#87676=LINE ( 'NONE', #101399, #44956 ) ;
#87677=ADVANCED_FACE ( 'NONE', ( #45663 ), #12974, .F. ) ;
#87678=ORIENTED_EDGE ( 'NONE', *, *, #61772, .T. ) ;
#87679=EDGE_LOOP ( 'NONE', ( #26488, #54141, #20778, #77280 ) ) ;
#87680=LINE ( 'NONE', #131910, #21305 ) ;
#87681=LINE ( 'NONE', #112305, #85725 ) ;
#87683=PLANE ( 'NONE',  #25571 ) ;
#87684=EDGE_CURVE ( 'NONE', #41910, #59525, #143504, .T. ) ;
#87685=VERTEX_POINT ( 'NONE', #110842 ) ;
#87686=DIRECTION ( 'NONE',  ( -0.6830127018922180770, -0.6830127018922204085, -0.2588190451025213501 ) ) ;
#87687=CARTESIAN_POINT ( 'NONE',  ( 24.18398860626899705, 28.73617430169804265, 5.000000000000000000 ) ) ;
#87689=ORIENTED_EDGE ( 'NONE', *, *, #103539, .F. ) ;
#87692=CARTESIAN_POINT ( 'NONE',  ( 54.48921356237310221, -27.52281430457093236, 5.000000000000000000 ) ) ;
#87693=CARTESIAN_POINT ( 'NONE',  ( 11.66989781452728359, 17.25929247661553845, 19.83885114516068526 ) ) ;
#87694=VERTEX_POINT ( 'NONE', #34763 ) ;
#87695=EDGE_CURVE ( 'NONE', #118868, #86890, #55815, .T. ) ;
#87697=ORIENTED_EDGE ( 'NONE', *, *, #87523, .T. ) ;
#87698=ORIENTED_EDGE ( 'NONE', *, *, #57122, .F. ) ;
#87699=CARTESIAN_POINT ( 'NONE',  ( -32.99999999999977263, 9.631307414974292769, -9.079085613539614741 ) ) ;
#87700=DIRECTION ( 'NONE',  ( -0.7071067811865487940, 0.7071067811865463515, 0.000000000000000000 ) ) ;
#87701=CARTESIAN_POINT ( 'NONE',  ( -15.79333936457836707, 21.75929247661549937, 4.998822639870700080 ) ) ;
#87703=VERTEX_POINT ( 'NONE', #56562 ) ;
#87704=EDGE_CURVE ( 'NONE', #52437, #84626, #89831, .T. ) ;
#87705=ADVANCED_FACE ( 'NONE', ( #90573 ), #134810, .T. ) ;
#87706=LINE ( 'NONE', #31903, #57620 ) ;
#87707=CARTESIAN_POINT ( 'NONE',  ( -28.49999999999979750, -10.53360074219763121, 5.000000000000000000 ) ) ;
#87709=ORIENTED_EDGE ( 'NONE', *, *, #58641, .T. ) ;
#87710=PLANE ( 'NONE',  #51262 ) ;
#87711=VECTOR ( 'NONE', #78086, 1000.000000000000000 ) ;
#87712=AXIS2_PLACEMENT_3D ( 'NONE', #102977, #1476, #59490 ) ;
#87713=PLANE ( 'NONE',  #104953 ) ;
#87714=ADVANCED_FACE ( 'NONE', ( #102874 ), #49221, .F. ) ;
#87715=ORIENTED_EDGE ( 'NONE', *, *, #29215, .F. ) ;
#87717=CARTESIAN_POINT ( 'NONE',  ( -9.299744871391588674, -27.71228299555212971, 4.000000000000000000 ) ) ;
#87718=ORIENTED_EDGE ( 'NONE', *, *, #110406, .T. ) ;
#87719=ADVANCED_FACE ( 'NONE', ( #116587 ), #93412, .F. ) ;
#87722=LINE ( 'NONE', #121752, #40079 ) ;
#87723=DIRECTION ( 'NONE',  ( -0.000000000000000000, 0.000000000000000000, 1.000000000000000000 ) ) ;
#87725=ORIENTED_EDGE ( 'NONE', *, *, #50685, .F. ) ;
#87726=DIRECTION ( 'NONE',  ( 1.000000000000000000, 0.000000000000000000, 0.000000000000000000 ) ) ;
#87728=CARTESIAN_POINT ( 'NONE',  ( -12.48921356237309155, -27.52281430457064104, 5.000000000000000000 ) ) ;
#87729=DIRECTION ( 'NONE',  ( -0.3543493200069162685, -0.000000000000000000, -0.9351131265310288487 ) ) ;
#87730=ADVANCED_FACE ( 'NONE', ( #15109 ), #60087, .F. ) ;
#87731=LINE ( 'NONE', #131966, #141127 ) ;
#87734=CARTESIAN_POINT ( 'NONE',  ( 29.99999999999979039, -6.412538124160685804, 4.000000000000000000 ) ) ;
#87735=FACE_OUTER_BOUND ( 'NONE', #24875, .T. ) ;
#87736=DIRECTION ( 'NONE',  ( -0.7071067811865487940, 0.7071067811865463515, 0.000000000000000000 ) ) ;
#87737=CARTESIAN_POINT ( 'NONE',  ( -34.92500000000001137, 10.33457404400604140, 0.4942731178106014589 ) ) ;
#87738=VECTOR ( 'NONE', #29060, 1000.000000000000000 ) ;
#87739=LINE ( 'NONE', #53702, #120094 ) ;
#87740=EDGE_CURVE ( 'NONE', #92540, #26964, #36873, .T. ) ;
#87742=CARTESIAN_POINT ( 'NONE',  ( -20.51078643762690490, -27.52281430457041012, 5.000000000000000000 ) ) ;
#87743=ORIENTED_EDGE ( 'NONE', *, *, #139462, .F. ) ;
#87747=ORIENTED_EDGE ( 'NONE', *, *, #86903, .T. ) ;
#87748=VERTEX_POINT ( 'NONE', #92675 ) ;
#87749=VERTEX_POINT ( 'NONE', #104989 ) ;
#87750=DIRECTION ( 'NONE',  ( 0.6830127018922181881, 0.6830127018922202975, -0.2588190451025214056 ) ) ;
#87752=ORIENTED_EDGE ( 'NONE', *, *, #71990, .T. ) ;
#87753=VECTOR ( 'NONE', #128613, 1000.000000000000000 ) ;
#87754=CARTESIAN_POINT ( 'NONE',  ( 34.42499999999998295, 22.22500000000000142, 5.000000000000000000 ) ) ;
#87756=VECTOR ( 'NONE', #96083, 1000.000000000000000 ) ;
#87757=CARTESIAN_POINT ( 'NONE',  ( 13.10742158956126246, 3.736470153597433619, 4.109745541549489012 ) ) ;
#87758=DIRECTION ( 'NONE',  ( -0.7071067811865486830, -0.7071067811865464625, 0.000000000000000000 ) ) ;
#87759=EDGE_LOOP ( 'NONE', ( #123255, #16115, #7756, #10063 ) ) ;
#87760=CARTESIAN_POINT ( 'NONE',  ( 0.7071067811865432429, 11.25929247661560595, 5.000000000000000000 ) ) ;
#87762=AXIS2_PLACEMENT_3D ( 'NONE', #94679, #138937, #54099 ) ;
#87765=CARTESIAN_POINT ( 'NONE',  ( 54.18398860626899705, 28.73617430169825226, 5.000000000000000000 ) ) ;
#87766=AXIS2_PLACEMENT_3D ( 'NONE', #74664, #99215, #19542 ) ;
#87768=CARTESIAN_POINT ( 'NONE',  ( -20.20666063542138957, 21.75929247661549226, 4.998822639870715179 ) ) ;
#87769=EDGE_CURVE ( 'NONE', #89080, #135397, #83252, .T. ) ;
#87770=ADVANCED_FACE ( 'NONE', ( #15792 ), #124611, .F. ) ;
#87771=ORIENTED_EDGE ( 'NONE', *, *, #19469, .T. ) ;
#87772=EDGE_LOOP ( 'NONE', ( #15359, #126910, #15739, #77521 ) ) ;
#87774=EDGE_LOOP ( 'NONE', ( #142209, #75207, #2450, #122008 ) ) ;
#87775=DIRECTION ( 'NONE',  ( -0.7071067811865486830, -0.7071067811865464625, 0.000000000000000000 ) ) ;
#87778=DIRECTION ( 'NONE',  ( -0.6830127018922181881, 0.6830127018922202975, -0.2588190451025214056 ) ) ;
#87779=FACE_OUTER_BOUND ( 'NONE', #104273, .T. ) ;
#87780=LINE ( 'NONE', #42874, #9597 ) ;
#87782=ORIENTED_EDGE ( 'NONE', *, *, #85485, .T. ) ;
#87783=VERTEX_POINT ( 'NONE', #104256 ) ;
#87785=DIRECTION ( 'NONE',  ( -0.7071067811865487940, 0.7071067811865463515, 0.000000000000000000 ) ) ;
#87786=VERTEX_POINT ( 'NONE', #4922 ) ;
#87787=ORIENTED_EDGE ( 'NONE', *, *, #42272, .T. ) ;
#87789=ORIENTED_EDGE ( 'NONE', *, *, #63957, .T. ) ;
#87790=CARTESIAN_POINT ( 'NONE',  ( -71.99451991528749772, 28.92564299267988304, 4.000000000000000000 ) ) ;
#87791=DIRECTION ( 'NONE',  ( -0.6830127018922180770, -0.6830127018922204085, -0.2588190451025213501 ) ) ;
#87792=LINE ( 'NONE', #757, #90076 ) ;
#87795=LINE ( 'NONE', #11628, #47924 ) ;
#87796=ORIENTED_EDGE ( 'NONE', *, *, #119010, .F. ) ;
#87798=EDGE_LOOP ( 'NONE', ( #52229, #79950, #103113, #114818 ) ) ;
#87799=PLANE ( 'NONE',  #109021 ) ;
#87800=ORIENTED_EDGE ( 'NONE', *, *, #61206, .T. ) ;
#87802=PLANE ( 'NONE',  #66819 ) ;
#87804=AXIS2_PLACEMENT_3D ( 'NONE', #49598, #28539, #48145 ) ;
#87805=VECTOR ( 'NONE', #138797, 1000.000000000000227 ) ;
#87806=CARTESIAN_POINT ( 'NONE',  ( -11.99451991528749417, 28.92564299267946382, 4.000000000000000000 ) ) ;
#87807=AXIS2_PLACEMENT_3D ( 'NONE', #96873, #30972, #6283 ) ;
#87808=ADVANCED_FACE ( 'NONE', ( #135507 ), #26722, .F. ) ;
#87809=FACE_BOUND ( 'NONE', #80167, .T. ) ;
#87810=ORIENTED_EDGE ( 'NONE', *, *, #23606, .T. ) ;
#87811=DIRECTION ( 'NONE',  ( -0.6830127018922180770, -0.6830127018922204085, -0.2588190451025213501 ) ) ;
#87812=EDGE_CURVE ( 'NONE', #57315, #67596, #91978, .T. ) ;
#87813=EDGE_CURVE ( 'NONE', #44987, #108750, #49927, .T. ) ;
#87814=DIRECTION ( 'NONE',  ( 0.7071067811865486830, -0.7071067811865464625, -0.000000000000000000 ) ) ;
#87815=DIRECTION ( 'NONE',  ( -0.6830127018922180770, -0.6830127018922204085, -0.2588190451025213501 ) ) ;
#87816=EDGE_LOOP ( 'NONE', ( #134372, #105830, #78716 ) ) ;
#87818=VERTEX_POINT ( 'NONE', #27416 ) ;
#87820=VECTOR ( 'NONE', #74914, 1000.000000000000000 ) ;
#87821=CARTESIAN_POINT ( 'NONE',  ( 14.99999999999989875, 20.96639925780205260, 5.000000000000000000 ) ) ;
#87822=EDGE_LOOP ( 'NONE', ( #85667, #34653, #136930, #39795 ) ) ;
#87824=EDGE_CURVE ( 'NONE', #119486, #57481, #96230, .T. ) ;
#87826=ORIENTED_EDGE ( 'NONE', *, *, #4694, .T. ) ;
#87828=FACE_OUTER_BOUND ( 'NONE', #95397, .T. ) ;
#87829=ADVANCED_FACE ( 'NONE', ( #28876 ), #107826, .F. ) ;
#87830=DIRECTION ( 'NONE',  ( -0.000000000000000000, 0.3543493200069153248, 0.9351131265310292928 ) ) ;
#87831=ORIENTED_EDGE ( 'NONE', *, *, #140939, .T. ) ;
#87833=PLANE ( 'NONE',  #143021 ) ;
#87834=VECTOR ( 'NONE', #119797, 1000.000000000000000 ) ;
#87835=ADVANCED_FACE ( 'NONE', ( #96934 ), #120117, .F. ) ;
#87836=VECTOR ( 'NONE', #139502, 1000.000000000000227 ) ;
#87838=CYLINDRICAL_SURFACE ( 'NONE', #62153, 0.5000000000000000000 ) ;
#87839=CARTESIAN_POINT ( 'NONE',  ( 11.99451991528749417, 28.92564299267946382, 4.000000000000000000 ) ) ;
#87840=PLANE ( 'NONE',  #2923 ) ;
#87841=LINE ( 'NONE', #77697, #83489 ) ;
#87842=ORIENTED_EDGE ( 'NONE', *, *, #13058, .F. ) ;
#87843=EDGE_LOOP ( 'NONE', ( #140531, #16221, #7870, #53441 ) ) ;
#87844=ORIENTED_EDGE ( 'NONE', *, *, #71887, .T. ) ;
#87845=VECTOR ( 'NONE', #85810, 999.9999999999998863 ) ;
#87846=CARTESIAN_POINT ( 'NONE',  ( 14.84387692260749603, -22.22499999999999432, 4.000000000000000000 ) ) ;
#87847=CARTESIAN_POINT ( 'NONE',  ( 15.48921356237309510, -27.52281430457066236, 5.000000000000000000 ) ) ;
#87848=VERTEX_POINT ( 'NONE', #128882 ) ;
#87850=AXIS2_PLACEMENT_3D ( 'NONE', #81333, #125541, #15296 ) ;
#87851=ORIENTED_EDGE ( 'NONE', *, *, #32017, .F. ) ;
#87853=DIRECTION ( 'NONE',  ( 0.6830127018922181881, 0.6830127018922202975, -0.2588190451025214056 ) ) ;
#87855=ORIENTED_EDGE ( 'NONE', *, *, #46178, .T. ) ;
#87856=VECTOR ( 'NONE', #141213, 1000.000000000000000 ) ;
#87857=DIRECTION ( 'NONE',  ( -0.7071067811865486830, -0.7071067811865464625, 0.000000000000000000 ) ) ;
#87858=EDGE_CURVE ( 'NONE', #9764, #105676, #39886, .T. ) ;
#87859=VECTOR ( 'NONE', #90740, 999.9999999999998863 ) ;
#87860=LINE ( 'NONE', #65427, #81514 ) ;
#87862=LINE ( 'NONE', #21884, #38914 ) ;
#87863=ORIENTED_EDGE ( 'NONE', *, *, #115107, .F. ) ;
#87865=CARTESIAN_POINT ( 'NONE',  ( 20.99451991528748707, 28.92564299267952777, 4.000000000000000000 ) ) ;
#87866=EDGE_CURVE ( 'NONE', #4116, #45577, #52741, .T. ) ;
#87867=DIRECTION ( 'NONE',  ( 0.7071067811865486830, -0.7071067811865464625, -0.000000000000000000 ) ) ;
#87868=VECTOR ( 'NONE', #5338, 1000.000000000000000 ) ;
#87869=LINE ( 'NONE', #21180, #72674 ) ;
#87870=ORIENTED_EDGE ( 'NONE', *, *, #106011, .T. ) ;
#87871=CARTESIAN_POINT ( 'NONE',  ( 21.18398860626899349, 28.73617430169802134, 5.000000000000000000 ) ) ;
#87872=VERTEX_POINT ( 'NONE', #42628 ) ;
#87873=CARTESIAN_POINT ( 'NONE',  ( -10.49999999999992184, -4.912538124160708897, 4.000000000000000000 ) ) ;
#87875=DIRECTION ( 'NONE',  ( 0.7071067811865486830, -0.7071067811865464625, -0.000000000000000000 ) ) ;
#87876=ORIENTED_EDGE ( 'NONE', *, *, #56116, .F. ) ;
#87877=EDGE_CURVE ( 'NONE', #2199, #57761, #108523, .T. ) ;
#87878=EDGE_CURVE ( 'NONE', #30701, #79059, #75943, .T. ) ;
#87879=CARTESIAN_POINT ( 'NONE',  ( -26.99999999999981526, 9.631307414974299874, -9.079085613539605859 ) ) ;
#87880=DIRECTION ( 'NONE',  ( -0.6830127018922180770, -0.6830127018922204085, -0.2588190451025213501 ) ) ;
#87881=ORIENTED_EDGE ( 'NONE', *, *, #71991, .F. ) ;
#87882=CARTESIAN_POINT ( 'NONE',  ( 7.499999999999951150, 7.087461875839168535, 4.000000000000000000 ) ) ;
#87883=DIRECTION ( 'NONE',  ( 1.000000000000000000, -0.000000000000000000, -0.000000000000000000 ) ) ;
#87884=EDGE_CURVE ( 'NONE', #4046, #12348, #139067, .T. ) ;
#87885=ORIENTED_EDGE ( 'NONE', *, *, #141796, .T. ) ;
#87886=DIRECTION ( 'NONE',  ( 0.000000000000000000, 0.000000000000000000, 1.000000000000000000 ) ) ;
#87887=FACE_OUTER_BOUND ( 'NONE', #15005, .T. ) ;
#87888=VERTEX_POINT ( 'NONE', #73801 ) ;
#87891=CARTESIAN_POINT ( 'NONE',  ( -21.79289321881330466, -14.24070752338413470, 5.000000000000000000 ) ) ;
#87892=VERTEX_POINT ( 'NONE', #118717 ) ;
#87894=CARTESIAN_POINT ( 'NONE',  ( 0.4892135623730947680, -27.52281430457055578, 5.000000000000000000 ) ) ;
#87895=ORIENTED_EDGE ( 'NONE', *, *, #136766, .T. ) ;
#87897=CARTESIAN_POINT ( 'NONE',  ( -3.183988606268992161, 28.73617430169789699, 5.000000000000000000 ) ) ;
#87898=CARTESIAN_POINT ( 'NONE',  ( 0.000000000000000000, 0.000000000000000000, 5.000000000000000000 ) ) ;
#87902=DIRECTION ( 'NONE',  ( 0.3543493200069163240, -0.000000000000000000, -0.9351131265310288487 ) ) ;
#87903=ORIENTED_EDGE ( 'NONE', *, *, #118593, .F. ) ;
#87904=ORIENTED_EDGE ( 'NONE', *, *, #102782, .T. ) ;
#87906=ORIENTED_EDGE ( 'NONE', *, *, #136078, .F. ) ;
#87907=ORIENTED_EDGE ( 'NONE', *, *, #20410, .F. ) ;
#87908=CARTESIAN_POINT ( 'NONE',  ( -44.99451991528749772, 28.92564299267969474, 4.000000000000000000 ) ) ;
#87909=DIRECTION ( 'NONE',  ( 0.6830127018922180770, -0.6830127018922204085, -0.2588190451025213501 ) ) ;
#87911=VECTOR ( 'NONE', #23687, 1000.000000000000227 ) ;
#87913=ORIENTED_EDGE ( 'NONE', *, *, #73162, .T. ) ;
#87914=CARTESIAN_POINT ( 'NONE',  ( 0.000000000000000000, 0.000000000000000000, 5.000000000000000000 ) ) ;
#87915=DIRECTION ( 'NONE',  ( 0.7071067811865487940, 0.7071067811865463515, 0.000000000000000000 ) ) ;
#87917=CARTESIAN_POINT ( 'NONE',  ( 27.79289321881326913, 12.75929247661559351, 5.000000000000000000 ) ) ;
#87918=EDGE_CURVE ( 'NONE', #29863, #118228, #31723, .T. ) ;
#87919=DIRECTION ( 'NONE',  ( 0.7071067811865487940, 0.7071067811865463515, -0.000000000000000000 ) ) ;
#87922=LINE ( 'NONE', #85774, #44188 ) ;
#87923=CARTESIAN_POINT ( 'NONE',  ( 4.499999999999976019, -8.947814304570735899, 5.000000000000000000 ) ) ;
#87925=DIRECTION ( 'NONE',  ( 0.6830127018922180770, -0.6830127018922204085, -0.2588190451025213501 ) ) ;
#87927=LINE ( 'NONE', #11044, #92140 ) ;
#87930=ADVANCED_FACE ( 'NONE', ( #41162 ), #20826, .F. ) ;
#87931=CARTESIAN_POINT ( 'NONE',  ( -24.83829387547365286, -6.740707523384205757, 16.75550250614861625 ) ) ;
#87932=AXIS2_PLACEMENT_3D ( 'NONE', #91304, #81864, #26725 ) ;
#87933=ORIENTED_EDGE ( 'NONE', *, *, #58045, .F. ) ;
#87936=EDGE_CURVE ( 'NONE', #74056, #94977, #84000, .T. ) ;
#87937=DIRECTION ( 'NONE',  ( -0.6830127018922180770, -0.6830127018922204085, -0.2588190451025213501 ) ) ;
#87941=LINE ( 'NONE', #99506, #138136 ) ;
#87942=DIRECTION ( 'NONE',  ( 0.7071067811865487940, 0.7071067811865463515, 0.000000000000000000 ) ) ;
#87944=EDGE_CURVE ( 'NONE', #124953, #70498, #73112, .T. ) ;
#87946=ORIENTED_EDGE ( 'NONE', *, *, #86869, .T. ) ;
#87948=EDGE_LOOP ( 'NONE', ( #87135, #17450, #104056, #50599, #97478 ) ) ;
#87949=ORIENTED_EDGE ( 'NONE', *, *, #110116, .T. ) ;
#87950=DIRECTION ( 'NONE',  ( 0.6830127018922180770, -0.6830127018922204085, -0.2588190451025213501 ) ) ;
#87952=VECTOR ( 'NONE', #44274, 1000.000000000000000 ) ;
#87954=CARTESIAN_POINT ( 'NONE',  ( -23.99999999999982947, -3.033600742197705369, 5.000000000000000000 ) ) ;
#87955=CARTESIAN_POINT ( 'NONE',  ( 32.99999999999976552, -13.06887692260767686, 4.000000000000000000 ) ) ;
#87956=VERTEX_POINT ( 'NONE', #77405 ) ;
#87957=EDGE_CURVE ( 'NONE', #129972, #103515, #55627, .T. ) ;
#87958=CARTESIAN_POINT ( 'NONE',  ( -33.48921356237309510, -27.52281430457078670, 5.000000000000000000 ) ) ;
#87960=ORIENTED_EDGE ( 'NONE', *, *, #116864, .T. ) ;
#87961=AXIS2_PLACEMENT_3D ( 'NONE', #134702, #47711, #91872 ) ;
#87963=LINE ( 'NONE', #97378, #69341 ) ;
#87964=DIRECTION ( 'NONE',  ( 0.7071067811865487940, 0.7071067811865463515, 0.000000000000000000 ) ) ;
#87965=DIRECTION ( 'NONE',  ( -0.000000000000000000, 0.3543493200069153248, 0.9351131265310292928 ) ) ;
#87966=AXIS2_PLACEMENT_3D ( 'NONE', #23564, #69230, #67833 ) ;
#87967=CARTESIAN_POINT ( 'NONE',  ( -18.18398860626898994, 28.73617430169800002, 5.000000000000000000 ) ) ;
#87969=EDGE_LOOP ( 'NONE', ( #72311, #49313, #92564, #11863 ) ) ;
#87970=CARTESIAN_POINT ( 'NONE',  ( 27.24169458425171086, 0.7592924766157138627, 14.37146558664976759 ) ) ;
#87972=LINE ( 'NONE', #90102, #48803 ) ;
#87973=CARTESIAN_POINT ( 'NONE',  ( -12.70710678118645021, 5.259292476615667233, 5.000000000000000000 ) ) ;
#87974=DIRECTION ( 'NONE',  ( 0.7071067811865487940, 0.7071067811865463515, -0.000000000000000000 ) ) ;
#87976=VERTEX_POINT ( 'NONE', #79565 ) ;
#87977=VECTOR ( 'NONE', #58923, 999.9999999999998863 ) ;
#87978=CARTESIAN_POINT ( 'NONE',  ( -6.183988606268994381, 28.73617430169791476, 5.000000000000000000 ) ) ;
#87979=CARTESIAN_POINT ( 'NONE',  ( 17.20829011259838026, -2.505970753447624322, 4.303104124266152297 ) ) ;
#87980=ORIENTED_EDGE ( 'NONE', *, *, #66664, .F. ) ;
#87981=ORIENTED_EDGE ( 'NONE', *, *, #11876, .T. ) ;
#87982=CARTESIAN_POINT ( 'NONE',  ( -34.42500000000001137, 17.97718569542923106, 5.000000000000000000 ) ) ;
#87983=ORIENTED_EDGE ( 'NONE', *, *, #39229, .T. ) ;
#87984=LINE ( 'NONE', #44522, #33099 ) ;
#87985=CARTESIAN_POINT ( 'NONE',  ( 29.67183060077626422, 14.25929247661556509, 4.000000000000000000 ) ) ;
#87986=VECTOR ( 'NONE', #117591, 1000.000000000000000 ) ;
#87987=ADVANCED_FACE ( 'NONE', ( #88255 ), #134628, .F. ) ;
#87988=LINE ( 'NONE', #132238, #28029 ) ;
#87989=FACE_BOUND ( 'NONE', #137591, .T. ) ;
#87990=DIRECTION ( 'NONE',  ( 2.781805975412905274E-17, -0.3543493200069152138, 0.9351131265310292928 ) ) ;
#87991=ADVANCED_FACE ( 'NONE', ( #109986 ), #11352, .F. ) ;
#87993=LINE ( 'NONE', #56118, #75846 ) ;
#87994=DIRECTION ( 'NONE',  ( -0.3543493200069162685, -0.000000000000000000, -0.9351131265310288487 ) ) ;
#87995=ORIENTED_EDGE ( 'NONE', *, *, #15532, .T. ) ;
#87996=AXIS2_PLACEMENT_3D ( 'NONE', #35341, #14265, #22963 ) ;
#87997=PLANE ( 'NONE',  #81054 ) ;
#87998=ORIENTED_EDGE ( 'NONE', *, *, #17465, .F. ) ;
#87999=ADVANCED_FACE ( 'NONE', ( #1892 ), #87532, .F. ) ;
#88001=ORIENTED_EDGE ( 'NONE', *, *, #122830, .T. ) ;
#88003=ORIENTED_EDGE ( 'NONE', *, *, #37550, .T. ) ;
#88004=EDGE_CURVE ( 'NONE', #69590, #115675, #54227, .T. ) ;
#88005=CARTESIAN_POINT ( 'NONE',  ( 3.792893218813427669, 15.75929247661555976, 5.000000000000000000 ) ) ;
#88007=ORIENTED_EDGE ( 'NONE', *, *, #108330, .F. ) ;
#88008=FACE_OUTER_BOUND ( 'NONE', #77677, .T. ) ;
#88009=EDGE_CURVE ( 'NONE', #51675, #133359, #76683, .T. ) ;
#88011=CARTESIAN_POINT ( 'NONE',  ( 24.18398860626899705, 28.73617430169804265, 5.000000000000000000 ) ) ;
#88014=FACE_OUTER_BOUND ( 'NONE', #38403, .T. ) ;
#88015=CARTESIAN_POINT ( 'NONE',  ( -9.005480084712511157, 28.92564299267931816, 4.000000000000000000 ) ) ;
#88016=CARTESIAN_POINT ( 'NONE',  ( -6.183988606268994381, 28.73617430169791476, 5.000000000000000000 ) ) ;
#88017=CARTESIAN_POINT ( 'NONE',  ( -24.75860074219779605, 21.72500000000000853, 5.000000000000000000 ) ) ;
#88018=FACE_OUTER_BOUND ( 'NONE', #134763, .T. ) ;
#88019=ORIENTED_EDGE ( 'NONE', *, *, #106579, .F. ) ;
#88020=VECTOR ( 'NONE', #46398, 1000.000000000000000 ) ;
#88023=ORIENTED_EDGE ( 'NONE', *, *, #129381, .T. ) ;
#88024=CARTESIAN_POINT ( 'NONE',  ( -66.18398860626901126, 28.73617430169833753, 5.000000000000000000 ) ) ;
#88025=CARTESIAN_POINT ( 'NONE',  ( -27.48921356237309155, -27.52281430457074762, 5.000000000000000000 ) ) ;
#88027=EDGE_CURVE ( 'NONE', #133213, #5707, #123752, .T. ) ;
#88028=ORIENTED_EDGE ( 'NONE', *, *, #70984, .T. ) ;
#88029=ORIENTED_EDGE ( 'NONE', *, *, #130967, .F. ) ;
#88030=CARTESIAN_POINT ( 'NONE',  ( 9.489213562373095101, -27.52281430457062328, 5.000000000000000000 ) ) ;
#88031=ORIENTED_EDGE ( 'NONE', *, *, #87175, .T. ) ;
#88033=CARTESIAN_POINT ( 'NONE',  ( 32.99999999999977973, -13.44781430457069149, 5.000000000000000000 ) ) ;
#88034=EDGE_CURVE ( 'NONE', #57989, #22749, #1206, .T. ) ;
#88035=DIRECTION ( 'NONE',  ( 0.3543493200069164351, 2.781805975412904658E-17, -0.9351131265310288487 ) ) ;
#88039=CARTESIAN_POINT ( 'NONE',  ( -16.49999999999987921, -8.947814304570734123, 5.000000000000000000 ) ) ;
#88040=ORIENTED_EDGE ( 'NONE', *, *, #57801, .T. ) ;
#88041=LINE ( 'NONE', #122074, #90511 ) ;
#88042=CARTESIAN_POINT ( 'NONE',  ( 29.99451991528749417, 28.92564299267958816, 4.000000000000000000 ) ) ;
#88043=FACE_OUTER_BOUND ( 'NONE', #89237, .T. ) ;
#88044=ORIENTED_EDGE ( 'NONE', *, *, #24795, .F. ) ;
#88045=ORIENTED_EDGE ( 'NONE', *, *, #139992, .T. ) ;
#88046=DIRECTION ( 'NONE',  ( -0.7071067811865486830, 0.7071067811865464625, 0.000000000000000000 ) ) ;
#88047=DIRECTION ( 'NONE',  ( 0.6830127018922181881, 0.6830127018922202975, -0.2588190451025214056 ) ) ;
#88048=CARTESIAN_POINT ( 'NONE',  ( -19.05000000000000071, 3.174999999999997158, 5.000000000000000000 ) ) ;
#88049=ORIENTED_EDGE ( 'NONE', *, *, #133515, .F. ) ;
#88051=PLANE ( 'NONE',  #140688 ) ;
#88052=AXIS2_PLACEMENT_3D ( 'NONE', #93002, #71995, #115419 ) ;
#88053=VERTEX_POINT ( 'NONE', #65088 ) ;
#88055=EDGE_CURVE ( 'NONE', #120179, #70500, #12095, .T. ) ;
#88056=AXIS2_PLACEMENT_3D ( 'NONE', #117658, #6037, #140175 ) ;
#88057=CARTESIAN_POINT ( 'NONE',  ( -0.7071067811865345831, -0.7407075233842753681, 5.000000000000000000 ) ) ;
#88058=CARTESIAN_POINT ( 'NONE',  ( 21.79289321881331176, -11.24070752338416845, 5.000000000000000000 ) ) ;
#88059=DIRECTION ( 'NONE',  ( -0.3543493200069162685, -0.000000000000000000, -0.9351131265310288487 ) ) ;
#88060=VECTOR ( 'NONE', #141769, 1000.000000000000227 ) ;
#88062=EDGE_CURVE ( 'NONE', #34692, #64188, #43322, .T. ) ;
#88063=LINE ( 'NONE', #122094, #116251 ) ;
#88064=LINE ( 'NONE', #77904, #19333 ) ;
#88065=DIRECTION ( 'NONE',  ( 0.7071067811865487940, 0.7071067811865463515, 0.000000000000000000 ) ) ;
#88066=ORIENTED_EDGE ( 'NONE', *, *, #46501, .T. ) ;
#88067=AXIS2_PLACEMENT_3D ( 'NONE', #27248, #115659, #16354 ) ;
#88068=DIRECTION ( 'NONE',  ( 0.6830127018922181881, 0.6830127018922202975, -0.2588190451025214056 ) ) ;
#88069=ORIENTED_EDGE ( 'NONE', *, *, #17332, .T. ) ;
#88070=DIRECTION ( 'NONE',  ( 0.7071067811865486830, -0.7071067811865464625, -0.000000000000000000 ) ) ;
#88071=EDGE_CURVE ( 'NONE', #36268, #48744, #101255, .T. ) ;
#88072=CARTESIAN_POINT ( 'NONE',  ( 0.000000000000000000, 0.000000000000000000, 5.000000000000000000 ) ) ;
#88073=DIRECTION ( 'NONE',  ( -0.6830127018922181881, 0.6830127018922202975, -0.2588190451025214056 ) ) ;
#88074=ORIENTED_EDGE ( 'NONE', *, *, #140379, .F. ) ;
#88076=CARTESIAN_POINT ( 'NONE',  ( -41.99451991528749062, 28.92564299267967343, 4.000000000000000000 ) ) ;
#88077=DIRECTION ( 'NONE',  ( -0.3543493200069162685, -0.000000000000000000, -0.9351131265310288487 ) ) ;
#88079=ORIENTED_EDGE ( 'NONE', *, *, #73920, .F. ) ;
#88080=ORIENTED_EDGE ( 'NONE', *, *, #69123, .F. ) ;
#88081=ADVANCED_FACE ( 'NONE', ( #123021 ), #12804, .F. ) ;
#88082=LINE ( 'NONE', #99645, #90442 ) ;
#88083=CARTESIAN_POINT ( 'NONE',  ( 34.42499999999998295, -21.02281430457037814, 5.000000000000000000 ) ) ;
#88084=AXIS2_PLACEMENT_3D ( 'NONE', #49279, #96273, #84050 ) ;
#88085=CARTESIAN_POINT ( 'NONE',  ( 51.48921356237309510, -27.52281430457091460, 5.000000000000000000 ) ) ;
#88086=DIRECTION ( 'NONE',  ( -1.000000000000000000, 0.000000000000000000, 0.000000000000000000 ) ) ;
#88087=FACE_OUTER_BOUND ( 'NONE', #51563, .T. ) ;
#88090=DIRECTION ( 'NONE',  ( -0.7071067811865486830, -0.7071067811865464625, 0.000000000000000000 ) ) ;
#88092=ORIENTED_EDGE ( 'NONE', *, *, #138169, .T. ) ;
#88093=DIRECTION ( 'NONE',  ( -0.000000000000000000, -0.3543493200069152693, 0.9351131265310292928 ) ) ;
#88096=DIRECTION ( 'NONE',  ( -0.6830127018922180770, -0.6830127018922204085, -0.2588190451025213501 ) ) ;
#88097=CARTESIAN_POINT ( 'NONE',  ( 0.000000000000000000, 0.000000000000000000, 5.000000000000000000 ) ) ;
#88098=LINE ( 'NONE', #133746, #113290 ) ;
#88099=LINE ( 'NONE', #121423, #7152 ) ;
#88101=ADVANCED_FACE ( 'NONE', ( #65824 ), #10652, .F. ) ;
#88102=DIRECTION ( 'NONE',  ( -0.000000000000000000, 0.3543493200069153248, 0.9351131265310292928 ) ) ;
#88103=DIRECTION ( 'NONE',  ( 0.3543493200069162685, -0.000000000000000000, -0.9351131265310288487 ) ) ;
#88104=ORIENTED_EDGE ( 'NONE', *, *, #13533, .F. ) ;
#88106=ORIENTED_EDGE ( 'NONE', *, *, #98226, .F. ) ;
#88110=VECTOR ( 'NONE', #99483, 1000.000000000000000 ) ;
#88111=DIRECTION ( 'NONE',  ( 1.000000000000000000, 0.000000000000000000, 0.000000000000000000 ) ) ;
#88114=FACE_OUTER_BOUND ( 'NONE', #79642, .T. ) ;
#88116=VERTEX_POINT ( 'NONE', #135344 ) ;
#88118=FACE_OUTER_BOUND ( 'NONE', #143216, .T. ) ;
#88120=DIRECTION ( 'NONE',  ( -0.000000000000000000, -0.3543493200069152693, 0.9351131265310292928 ) ) ;
#88121=EDGE_LOOP ( 'NONE', ( #120767, #55683, #105845 ) ) ;
#88123=DIRECTION ( 'NONE',  ( -0.7071067811865487940, 0.7071067811865463515, 0.000000000000000000 ) ) ;
#88125=ORIENTED_EDGE ( 'NONE', *, *, #112792, .T. ) ;
#88127=EDGE_CURVE ( 'NONE', #134968, #89060, #47640, .T. ) ;
#88128=CARTESIAN_POINT ( 'NONE',  ( -21.48921356237309155, -27.52281430457070499, 5.000000000000000000 ) ) ;
#88130=CARTESIAN_POINT ( 'NONE',  ( 26.52487387214937797, 14.25929247661557397, 9.797011795316699079 ) ) ;
#88131=ORIENTED_EDGE ( 'NONE', *, *, #50937, .F. ) ;
#88132=VECTOR ( 'NONE', #72605, 999.9999999999998863 ) ;
#88134=VECTOR ( 'NONE', #26720, 1000.000000000000000 ) ;
#88136=DIRECTION ( 'NONE',  ( -0.6830127018922180770, -0.6830127018922204085, -0.2588190451025213501 ) ) ;
#88137=( BOUNDED_CURVE ( )  B_SPLINE_CURVE ( 3, ( #7916, #19527, #139199, #18802 ),
 .UNSPECIFIED., .F., .T. ) 
 B_SPLINE_CURVE_WITH_KNOTS ( ( 4, 4 ),
 ( 1.864375635226946049, 1.933014472006540752 ),
 .UNSPECIFIED. ) 
 CURVE ( )  GEOMETRIC_REPRESENTATION_ITEM ( )  RATIONAL_B_SPLINE_CURVE ( ( 1.000000000000000000, 0.9996074310407766506, 0.9996074310407766506, 1.000000000000000000 ) ) 
 REPRESENTATION_ITEM ( '' )  );
#88138=VECTOR ( 'NONE', #83789, 1000.000000000000227 ) ;
#88139=CARTESIAN_POINT ( 'NONE',  ( 33.48921356237309510, -27.52281430457078670, 5.000000000000000000 ) ) ;
#88141=DIRECTION ( 'NONE',  ( -0.7071067811865487940, 0.7071067811865463515, -0.000000000000000000 ) ) ;
#88142=EDGE_CURVE ( 'NONE', #47388, #26153, #126562, .T. ) ;
#88143=PLANE ( 'NONE',  #69454 ) ;
#88144=DIRECTION ( 'NONE',  ( -0.6830127018922181881, 0.6830127018922202975, -0.2588190451025214056 ) ) ;
#88147=CARTESIAN_POINT ( 'NONE',  ( -1.499999999999984013, -5.947814304570766986, 5.000000000000000000 ) ) ;
#88148=CARTESIAN_POINT ( 'NONE',  ( 20.70025512860841133, -27.71228299555191654, 4.000000000000000000 ) ) ;
#88149=VECTOR ( 'NONE', #90627, 1000.000000000000000 ) ;
#88150=CARTESIAN_POINT ( 'NONE',  ( -28.49999999999980460, 9.431123077392088661, 4.000000000000000000 ) ) ;
#88151=EDGE_LOOP ( 'NONE', ( #50741, #69834, #49839, #24551 ) ) ;
#88152=VERTEX_POINT ( 'NONE', #27252 ) ;
#88154=ORIENTED_EDGE ( 'NONE', *, *, #126556, .F. ) ;
#88155=DIRECTION ( 'NONE',  ( -0.000000000000000000, 0.3543493200069153248, 0.9351131265310292928 ) ) ;
#88157=VECTOR ( 'NONE', #128047, 1000.000000000000000 ) ;
#88159=DIRECTION ( 'NONE',  ( 0.6830127018922180770, -0.6830127018922204085, -0.2588190451025213501 ) ) ;
#88160=ORIENTED_EDGE ( 'NONE', *, *, #114508, .F. ) ;
#88161=EDGE_LOOP ( 'NONE', ( #3123, #139739, #112946, #26508 ) ) ;
#88163=LINE ( 'NONE', #31636, #7264 ) ;
#88164=AXIS2_PLACEMENT_3D ( 'NONE', #51611, #95804, #140050 ) ;
#88165=ORIENTED_EDGE ( 'NONE', *, *, #48184, .F. ) ;
#88166=VECTOR ( 'NONE', #112731, 1000.000000000000000 ) ;
#88167=CARTESIAN_POINT ( 'NONE',  ( 0.7928932188134554249, -14.24070752338414003, 5.000000000000000000 ) ) ;
#88170=CARTESIAN_POINT ( 'NONE',  ( -8.700255128608413102, -27.71228299555199825, 4.000000000000000000 ) ) ;
#88171=AXIS2_PLACEMENT_3D ( 'NONE', #92335, #60482, #4567 ) ;
#88172=ORIENTED_EDGE ( 'NONE', *, *, #103498, .T. ) ;
#88173=FACE_BOUND ( 'NONE', #76785, .T. ) ;
#88174=CARTESIAN_POINT ( 'NONE',  ( 18.48921356237309510, -27.52281430457068367, 5.000000000000000000 ) ) ;
#88176=CARTESIAN_POINT ( 'NONE',  ( -24.48921356237309510, -27.52281430457072631, 5.000000000000000000 ) ) ;
#88177=LINE ( 'NONE', #20754, #92053 ) ;
#88178=CARTESIAN_POINT ( 'NONE',  ( 15.48921356237309510, -27.52281430457066236, 5.000000000000000000 ) ) ;
#88180=ORIENTED_EDGE ( 'NONE', *, *, #10555, .F. ) ;
#88181=EDGE_CURVE ( 'NONE', #136292, #70943, #25107, .T. ) ;
#88182=ORIENTED_EDGE ( 'NONE', *, *, #28110, .F. ) ;
#88184=EDGE_LOOP ( 'NONE', ( #104143, #75522, #81279, #8307 ) ) ;
#88185=ADVANCED_FACE ( 'NONE', ( #46939 ), #136024, .T. ) ;
#88186=EDGE_CURVE ( 'NONE', #109145, #123719, #49770, .T. ) ;
#88187=VERTEX_POINT ( 'NONE', #70803 ) ;
#88188=ADVANCED_FACE ( 'NONE', ( #69368 ), #68656, .F. ) ;
#88189=DIRECTION ( 'NONE',  ( -0.7071067811865486830, -0.7071067811865464625, 0.000000000000000000 ) ) ;
#88190=EDGE_CURVE ( 'NONE', #37517, #93975, #70114, .T. ) ;
#88191=PLANE ( 'NONE',  #57121 ) ;
#88192=PLANE ( 'NONE',  #59032 ) ;
#88193=ORIENTED_EDGE ( 'NONE', *, *, #92296, .F. ) ;
#88194=PLANE ( 'NONE',  #59996 ) ;
#88195=CARTESIAN_POINT ( 'NONE',  ( -66.18398860626901126, 28.73617430169833753, 5.000000000000000000 ) ) ;
#88197=EDGE_CURVE ( 'NONE', #134440, #44739, #91801, .T. ) ;
#88198=PLANE ( 'NONE',  #110499 ) ;
#88200=DIRECTION ( 'NONE',  ( 0.6830127018922180770, -0.6830127018922204085, -0.2588190451025213501 ) ) ;
#88201=VECTOR ( 'NONE', #71656, 999.9999999999998863 ) ;
#88202=DIRECTION ( 'NONE',  ( 0.7071067811865487940, 0.7071067811865463515, -0.000000000000000000 ) ) ;
#88203=ORIENTED_EDGE ( 'NONE', *, *, #91827, .T. ) ;
#88204=DIRECTION ( 'NONE',  ( -0.7071067811865486830, 0.7071067811865464625, 0.000000000000000000 ) ) ;
#88205=DIRECTION ( 'NONE',  ( 0.7071067811865487940, 0.7071067811865463515, -0.000000000000000000 ) ) ;
#88206=EDGE_CURVE ( 'NONE', #87113, #51885, #38865, .T. ) ;
#88207=EDGE_LOOP ( 'NONE', ( #141270, #138261, #117036, #69541 ) ) ;
#88208=ORIENTED_EDGE ( 'NONE', *, *, #78901, .T. ) ;
#88209=ADVANCED_FACE ( 'NONE', ( #80952 ), #83085, .T. ) ;
#88210=VERTEX_POINT ( 'NONE', #81685 ) ;
#88212=VECTOR ( 'NONE', #51402, 1000.000000000000000 ) ;
#88213=ORIENTED_EDGE ( 'NONE', *, *, #36660, .F. ) ;
#88215=CARTESIAN_POINT ( 'NONE',  ( 57.18398860626899705, 28.73617430169827358, 5.000000000000000000 ) ) ;
#88218=LINE ( 'NONE', #120819, #102999 ) ;
#88220=DIRECTION ( 'NONE',  ( -0.7071067811865486830, -0.7071067811865464625, 0.000000000000000000 ) ) ;
#88221=FACE_OUTER_BOUND ( 'NONE', #91554, .T. ) ;
#88222=LINE ( 'NONE', #101942, #76865 ) ;
#88223=CARTESIAN_POINT ( 'NONE',  ( 26.90156419391746923, 11.25929247661560240, 10.79108189686413333 ) ) ;
#88224=AXIS2_PLACEMENT_3D ( 'NONE', #55013, #50902, #95095 ) ;
#88225=ORIENTED_EDGE ( 'NONE', *, *, #31790, .T. ) ;
#88227=VERTEX_POINT ( 'NONE', #114275 ) ;
#88228=EDGE_LOOP ( 'NONE', ( #120140, #108532, #14372, #36090 ) ) ;
#88229=EDGE_CURVE ( 'NONE', #124891, #75364, #4738, .T. ) ;
#88231=VECTOR ( 'NONE', #91982, 1000.000000000000000 ) ;
#88232=AXIS2_PLACEMENT_3D ( 'NONE', #14806, #134465, #35169 ) ;
#88233=AXIS2_PLACEMENT_3D ( 'NONE', #28717, #29399, #52581 ) ;
#88234=VECTOR ( 'NONE', #13584, 1000.000000000000114 ) ;
#88235=VECTOR ( 'NONE', #141543, 999.9999999999998863 ) ;
#88236=CARTESIAN_POINT ( 'NONE',  ( 48.18398860626899705, 28.73617430169820608, 5.000000000000000000 ) ) ;
#88237=CARTESIAN_POINT ( 'NONE',  ( -7.499999999999944045, -19.91253812416055524, 4.000000000000000000 ) ) ;
#88238=VERTEX_POINT ( 'NONE', #114948 ) ;
#88239=FACE_OUTER_BOUND ( 'NONE', #61335, .T. ) ;
#88240=VECTOR ( 'NONE', #9842, 1000.000000000000000 ) ;
#88241=EDGE_LOOP ( 'NONE', ( #115050, #109254, #143052, #34288 ) ) ;
#88243=PLANE ( 'NONE',  #30051 ) ;
#88244=CARTESIAN_POINT ( 'NONE',  ( 45.48921356237309510, -27.52281430457087197, 5.000000000000000000 ) ) ;
#88246=PLANE ( 'NONE',  #55947 ) ;
#88247=EDGE_LOOP ( 'NONE', ( #66117, #140174, #22238, #22258 ) ) ;
#88248=ORIENTED_EDGE ( 'NONE', *, *, #108949, .T. ) ;
#88249=EDGE_CURVE ( 'NONE', #23176, #79521, #15627, .T. ) ;
#88250=ORIENTED_EDGE ( 'NONE', *, *, #28856, .T. ) ;
#88253=PLANE ( 'NONE',  #97291 ) ;
#88255=FACE_OUTER_BOUND ( 'NONE', #19227, .T. ) ;
#88256=DIRECTION ( 'NONE',  ( 1.000000000000000000, 0.000000000000000000, 0.000000000000000000 ) ) ;
#88259=DIRECTION ( 'NONE',  ( 2.781805975412906507E-17, 0.3543493200069153248, 0.9351131265310292928 ) ) ;
#88260=CARTESIAN_POINT ( 'NONE',  ( -13.49999999999990052, -13.53360074219760278, 5.000000000000000000 ) ) ;
#88262=LINE ( 'NONE', #67217, #9652 ) ;
#88263=LINE ( 'NONE', #132513, #83658 ) ;
#88264=AXIS2_PLACEMENT_3D ( 'NONE', #44922, #120987, #628 ) ;
#88265=ORIENTED_EDGE ( 'NONE', *, *, #94213, .T. ) ;
#88266=CARTESIAN_POINT ( 'NONE',  ( 39.18398860626899705, 28.73617430169814568, 5.000000000000000000 ) ) ;
#88267=VERTEX_POINT ( 'NONE', #5492 ) ;
#88268=DIRECTION ( 'NONE',  ( -0.7071067811865486830, -0.7071067811865464625, -0.000000000000000000 ) ) ;
#88273=VERTEX_POINT ( 'NONE', #93948 ) ;
#88275=VECTOR ( 'NONE', #102369, 999.9999999999998863 ) ;
#88276=CARTESIAN_POINT ( 'NONE',  ( 14.81601139373099585, 28.73617430169776910, 5.000000000000000000 ) ) ;
#88278=CARTESIAN_POINT ( 'NONE',  ( 15.18398860626900237, 28.73617430169797871, 5.000000000000000000 ) ) ;
#88279=VERTEX_POINT ( 'NONE', #6186 ) ;
#88280=CARTESIAN_POINT ( 'NONE',  ( 19.69064382391260892, -2.759520746520534473, 4.000000000000000000 ) ) ;
#88282=ORIENTED_EDGE ( 'NONE', *, *, #131278, .T. ) ;
#88283=CARTESIAN_POINT ( 'NONE',  ( 5.510786437626906675, -27.52281430457051314, 5.000000000000000000 ) ) ;
#88287=LINE ( 'NONE', #55660, #89908 ) ;
#88288=DIRECTION ( 'NONE',  ( -0.7071067811865486830, -0.7071067811865464625, 0.000000000000000000 ) ) ;
#88289=CARTESIAN_POINT ( 'NONE',  ( 4.499999999999966249, 11.52377502935403264, -1.522421517564095161 ) ) ;
#88290=PLANE ( 'NONE',  #85458 ) ;
#88292=VECTOR ( 'NONE', #115192, 1000.000000000000000 ) ;
#88294=DIRECTION ( 'NONE',  ( -0.000000000000000000, -0.3543493200069152693, 0.9351131265310292928 ) ) ;
#88295=AXIS2_PLACEMENT_3D ( 'NONE', #25114, #135354, #13515 ) ;
#88297=ORIENTED_EDGE ( 'NONE', *, *, #80588, .F. ) ;
#88298=ORIENTED_EDGE ( 'NONE', *, *, #45704, .F. ) ;
#88299=LINE ( 'NONE', #33237, #53677 ) ;
#88300=EDGE_LOOP ( 'NONE', ( #21873, #48417, #56954, #78509 ) ) ;
#88301=ADVANCED_FACE ( 'NONE', ( #18501 ), #9029, .T. ) ;
#88302=EDGE_CURVE ( 'NONE', #75268, #92497, #39597, .T. ) ;
#88303=AXIS2_PLACEMENT_3D ( 'NONE', #98460, #95598, #9262 ) ;
#88304=LINE ( 'NONE', #56427, #68879 ) ;
#88305=LINE ( 'NONE', #1252, #78736 ) ;
#88306=CARTESIAN_POINT ( 'NONE',  ( -16.17183060077635304, -2.240707523384264377, 4.000000000000000000 ) ) ;
#88307=VECTOR ( 'NONE', #9393, 1000.000000000000000 ) ;
#88308=FACE_OUTER_BOUND ( 'NONE', #118171, .T. ) ;
#88309=ORIENTED_EDGE ( 'NONE', *, *, #89271, .T. ) ;
#88310=DIRECTION ( 'NONE',  ( -0.7071067811865487940, 0.7071067811865463515, -0.000000000000000000 ) ) ;
#88312=CARTESIAN_POINT ( 'NONE',  ( -26.99451991528749417, 28.92564299267956685, 4.000000000000000000 ) ) ;
#88313=EDGE_CURVE ( 'NONE', #71584, #89949, #30865, .T. ) ;
#88314=EDGE_CURVE ( 'NONE', #143176, #70301, #107674, .T. ) ;
#88316=FACE_OUTER_BOUND ( 'NONE', #102976, .T. ) ;
#88317=ORIENTED_EDGE ( 'NONE', *, *, #22778, .T. ) ;
#88319=DIRECTION ( 'NONE',  ( -0.7071067811865487940, 0.7071067811865463515, -0.000000000000000000 ) ) ;
#88322=DIRECTION ( 'NONE',  ( 0.7071067811865487940, 0.7071067811865463515, -0.000000000000000000 ) ) ;
#88323=( BOUNDED_CURVE ( )  B_SPLINE_CURVE ( 3, ( #75555, #97252, #19723, #107446 ),
 .UNSPECIFIED., .F., .T. ) 
 B_SPLINE_CURVE_WITH_KNOTS ( ( 4, 4 ),
 ( 5.005968288816722733, 5.074607125596334534 ),
 .UNSPECIFIED. ) 
 CURVE ( )  GEOMETRIC_REPRESENTATION_ITEM ( )  RATIONAL_B_SPLINE_CURVE ( ( 1.000000000000000000, 0.9996074310407765395, 0.9996074310407765395, 1.000000000000000000 ) ) 
 REPRESENTATION_ITEM ( '' )  );
#88324=CARTESIAN_POINT ( 'NONE',  ( -6.299744871391586898, -27.71228299555210484, 4.000000000000000000 ) ) ;
#88325=VERTEX_POINT ( 'NONE', #129427 ) ;
#88326=EDGE_LOOP ( 'NONE', ( #2637, #37481, #134779 ) ) ;
#88327=ORIENTED_EDGE ( 'NONE', *, *, #88181, .F. ) ;
#88328=( BOUNDED_CURVE ( )  B_SPLINE_CURVE ( 3, ( #122452, #76118, #66676, #98569 ),
 .UNSPECIFIED., .F., .F. ) 
 B_SPLINE_CURVE_WITH_KNOTS ( ( 4, 4 ),
 ( 2.779374508378135378, 4.199602562396796301 ),
 .UNSPECIFIED. ) 
 CURVE ( )  GEOMETRIC_REPRESENTATION_ITEM ( )  RATIONAL_B_SPLINE_CURVE ( ( 1.000000000000000000, 0.8388583629366721528, 0.8388583629366721528, 1.000000000000000000 ) ) 
 REPRESENTATION_ITEM ( '' )  );
#88330=ORIENTED_EDGE ( 'NONE', *, *, #70071, .F. ) ;
#88333=ORIENTED_EDGE ( 'NONE', *, *, #29195, .T. ) ;
#88334=VECTOR ( 'NONE', #65081, 1000.000000000000000 ) ;
#88335=EDGE_CURVE ( 'NONE', #84441, #83371, #124959, .T. ) ;
#88339=AXIS2_PLACEMENT_3D ( 'NONE', #119869, #77153, #20574 ) ;
#88341=ORIENTED_EDGE ( 'NONE', *, *, #35720, .F. ) ;
#88342=FACE_OUTER_BOUND ( 'NONE', #51986, .T. ) ;
#88343=AXIS2_PLACEMENT_3D ( 'NONE', #95546, #128888, #116594 ) ;
#88346=AXIS2_PLACEMENT_3D ( 'NONE', #96248, #41181, #129614 ) ;
#88347=VECTOR ( 'NONE', #35408, 999.9999999999998863 ) ;
#88348=VECTOR ( 'NONE', #7241, 1000.000000000000000 ) ;
#88349=ORIENTED_EDGE ( 'NONE', *, *, #7019, .T. ) ;
#88350=ORIENTED_EDGE ( 'NONE', *, *, #119993, .T. ) ;
#88351=ORIENTED_EDGE ( 'NONE', *, *, #23331, .F. ) ;
#88352=DIRECTION ( 'NONE',  ( 1.000000000000000000, 0.000000000000000000, 0.000000000000000000 ) ) ;
#88353=DIRECTION ( 'NONE',  ( -0.000000000000000000, 0.3543493200069153248, 0.9351131265310292928 ) ) ;
#88354=DIRECTION ( 'NONE',  ( 0.7071067811865486830, -0.7071067811865464625, -0.000000000000000000 ) ) ;
#88355=AXIS2_PLACEMENT_3D ( 'NONE', #60528, #59112, #105407 ) ;
#88356=DIRECTION ( 'NONE',  ( -0.7071067811865487940, 0.7071067811865463515, -0.000000000000000000 ) ) ;
#88357=LINE ( 'NONE', #121658, #104259 ) ;
#88358=CARTESIAN_POINT ( 'NONE',  ( -27.80025329279436264, -22.22500000000000142, 2.300167135621889791 ) ) ;
#88361=VERTEX_POINT ( 'NONE', #8334 ) ;
#88362=VECTOR ( 'NONE', #11845, 1000.000000000000000 ) ;
#88363=ADVANCED_FACE ( 'NONE', ( #72963 ), #117812, .F. ) ;
#88364=ORIENTED_EDGE ( 'NONE', *, *, #114951, .T. ) ;
#88365=EDGE_LOOP ( 'NONE', ( #136968, #5447, #41480, #12948 ) ) ;
#88366=ADVANCED_FACE ( 'NONE', ( #141013 ), #72256, .F. ) ;
#88368=AXIS2_PLACEMENT_3D ( 'NONE', #76057, #64460, #55031 ) ;
#88369=VECTOR ( 'NONE', #109902, 1000.000000000000000 ) ;
#88370=EDGE_LOOP ( 'NONE', ( #503, #22589, #91984, #30379 ) ) ;
#88371=FACE_OUTER_BOUND ( 'NONE', #105629, .T. ) ;
#88372=LINE ( 'NONE', #98510, #32206 ) ;
#88373=AXIS2_PLACEMENT_3D ( 'NONE', #49379, #81281, #60243 ) ;
#88374=DIRECTION ( 'NONE',  ( -0.3543493200069162685, -0.000000000000000000, -0.9351131265310288487 ) ) ;
#88375=DIRECTION ( 'NONE',  ( -0.6830127018922180770, -0.6830127018922204085, -0.2588190451025213501 ) ) ;
#88376=AXIS2_PLACEMENT_3D ( 'NONE', #139108, #106417, #95578 ) ;
#88378=VERTEX_POINT ( 'NONE', #83831 ) ;
#88379=CARTESIAN_POINT ( 'NONE',  ( 30.18398860626900060, 28.73617430169808173, 5.000000000000000000 ) ) ;
#88380=EDGE_CURVE ( 'NONE', #89658, #103863, #97504, .T. ) ;
#88384=PLANE ( 'NONE',  #39915 ) ;
#88385=EDGE_CURVE ( 'NONE', #100921, #71118, #21231, .T. ) ;
#88386=ORIENTED_EDGE ( 'NONE', *, *, #120509, .T. ) ;
#88387=DIRECTION ( 'NONE',  ( 0.7071067811865487940, 0.7071067811865463515, 0.000000000000000000 ) ) ;
#88388=ORIENTED_EDGE ( 'NONE', *, *, #91236, .F. ) ;
#88390=AXIS2_PLACEMENT_3D ( 'NONE', #101735, #24185, #77167 ) ;
#88391=VERTEX_POINT ( 'NONE', #127287 ) ;
#88392=EDGE_CURVE ( 'NONE', #31545, #60397, #116426, .T. ) ;
#88393=DIRECTION ( 'NONE',  ( 1.000000000000000000, 0.000000000000000000, 0.000000000000000000 ) ) ;
#88395=CARTESIAN_POINT ( 'NONE',  ( 33.48921356237309510, -27.52281430457078670, 5.000000000000000000 ) ) ;
#88397=DIRECTION ( 'NONE',  ( -0.7071067811865486830, 0.7071067811865464625, 0.000000000000000000 ) ) ;
#88399=DIRECTION ( 'NONE',  ( 0.7071067811865487940, 0.7071067811865463515, 0.000000000000000000 ) ) ;
#88400=EDGE_CURVE ( 'NONE', #4583, #32218, #61380, .T. ) ;
#88401=VECTOR ( 'NONE', #95919, 1000.000000000000000 ) ;
#88402=DIRECTION ( 'NONE',  ( -0.7071067811865486830, -0.7071067811865464625, 0.000000000000000000 ) ) ;
#88403=PLANE ( 'NONE',  #96820 ) ;
#88404=DIRECTION ( 'NONE',  ( 0.7071067811865486830, -0.7071067811865464625, -0.000000000000000000 ) ) ;
#88405=CARTESIAN_POINT ( 'NONE',  ( 0.000000000000000000, 0.000000000000000000, 5.000000000000000000 ) ) ;
#88406=VERTEX_POINT ( 'NONE', #50462 ) ;
#88407=EDGE_LOOP ( 'NONE', ( #137925, #69562, #124203, #98390, #66456, #133801 ) ) ;
#88409=ORIENTED_EDGE ( 'NONE', *, *, #53866, .T. ) ;
#88411=CARTESIAN_POINT ( 'NONE',  ( 41.99451991528749062, 28.92564299267967343, 4.000000000000000000 ) ) ;
#88412=VERTEX_POINT ( 'NONE', #128039 ) ;
#88413=ORIENTED_EDGE ( 'NONE', *, *, #38590, .F. ) ;
#88414=LINE ( 'NONE', #78250, #111647 ) ;
#88415=CARTESIAN_POINT ( 'NONE',  ( 12.70710678118645731, -9.740707523384184441, 5.000000000000000000 ) ) ;
#88416=CARTESIAN_POINT ( 'NONE',  ( -28.49999999999979750, -1.912538124160733766, 4.000000000000000000 ) ) ;
#88417=DIRECTION ( 'NONE',  ( 0.6830127018922181881, 0.6830127018922202975, -0.2588190451025214056 ) ) ;
#88418=EDGE_CURVE ( 'NONE', #63455, #50077, #140318, .T. ) ;
#88419=ORIENTED_EDGE ( 'NONE', *, *, #58124, .F. ) ;
#88420=EDGE_CURVE ( 'NONE', #114304, #17773, #143168, .T. ) ;
#88422=VERTEX_POINT ( 'NONE', #58172 ) ;
#88423=CARTESIAN_POINT ( 'NONE',  ( 13.49999999999990408, -13.91253812416061386, 4.000000000000000000 ) ) ;
#88426=VERTEX_POINT ( 'NONE', #87373 ) ;
#88430=ORIENTED_EDGE ( 'NONE', *, *, #81805, .F. ) ;
#88431=CARTESIAN_POINT ( 'NONE',  ( -2.999999999999981792, 14.58746187583910903, 4.000000000000000000 ) ) ;
#88432=VERTEX_POINT ( 'NONE', #65664 ) ;
#88433=ORIENTED_EDGE ( 'NONE', *, *, #79015, .F. ) ;
#88434=DIRECTION ( 'NONE',  ( -0.000000000000000000, 0.3543493200069153248, 0.9351131265310292928 ) ) ;
#88435=DIRECTION ( 'NONE',  ( -0.3543493200069162685, -0.000000000000000000, -0.9351131265310288487 ) ) ;
#88436=DIRECTION ( 'NONE',  ( 0.7071067811865487940, 0.7071067811865463515, -0.000000000000000000 ) ) ;
#88437=VECTOR ( 'NONE', #58132, 1000.000000000000000 ) ;
#88438=DIRECTION ( 'NONE',  ( 0.6830127018922181881, 0.6830127018922202975, -0.2588190451025214056 ) ) ;
#88439=CARTESIAN_POINT ( 'NONE',  ( 42.48921356237308800, -27.52281430457085065, 5.000000000000000000 ) ) ;
#88440=ORIENTED_EDGE ( 'NONE', *, *, #67840, .T. ) ;
#88441=VECTOR ( 'NONE', #112812, 999.9999999999998863 ) ;
#88443=VECTOR ( 'NONE', #45, 1000.000000000000227 ) ;
#88444=CARTESIAN_POINT ( 'NONE',  ( -60.29974487139158867, -27.71228299555248142, 4.000000000000000000 ) ) ;
#88446=CARTESIAN_POINT ( 'NONE',  ( -45.48921356237309510, -27.52281430457087197, 5.000000000000000000 ) ) ;
#88448=VECTOR ( 'NONE', #96103, 1000.000000000000000 ) ;
#88450=VECTOR ( 'NONE', #25346, 1000.000000000000000 ) ;
#88451=DIRECTION ( 'NONE',  ( -0.6830127018922180770, -0.6830127018922204085, -0.2588190451025213501 ) ) ;
#88452=ORIENTED_EDGE ( 'NONE', *, *, #132595, .T. ) ;
#88453=DIRECTION ( 'NONE',  ( 0.7071067811865487940, 0.7071067811865463515, 0.000000000000000000 ) ) ;
#88454=ORIENTED_EDGE ( 'NONE', *, *, #139782, .T. ) ;
#88455=ORIENTED_EDGE ( 'NONE', *, *, #30766, .F. ) ;
#88456=CARTESIAN_POINT ( 'NONE',  ( 37.96659967656954393, 6.759292476615656575, 12.28218704918530868 ) ) ;
#88457=CARTESIAN_POINT ( 'NONE',  ( 72.48921356237309510, -27.52281430457106026, 5.000000000000000000 ) ) ;
#88458=ORIENTED_EDGE ( 'NONE', *, *, #142457, .F. ) ;
#88460=CARTESIAN_POINT ( 'NONE',  ( -34.92500000000001137, 22.22500000000000142, 4.000000000000000000 ) ) ;
#88461=CARTESIAN_POINT ( 'NONE',  ( 28.74845587132407587, -11.24070752338416135, 10.39518518046002704 ) ) ;
#88462=FACE_OUTER_BOUND ( 'NONE', #18813, .T. ) ;
#88463=LINE ( 'NONE', #132704, #14155 ) ;
#88464=DIRECTION ( 'NONE',  ( 0.7071067811865487940, 0.7071067811865463515, -0.000000000000000000 ) ) ;
#88465=LINE ( 'NONE', #132707, #33325 ) ;
#88466=DIRECTION ( 'NONE',  ( 0.7071067811865487940, 0.7071067811865463515, -0.000000000000000000 ) ) ;
#88468=CARTESIAN_POINT ( 'NONE',  ( -34.92382263987071411, 21.75929247661549226, 4.252424926123421933 ) ) ;
#88469=CARTESIAN_POINT ( 'NONE',  ( 9.156123077392344101, -22.22500000000000142, 4.000000000000000000 ) ) ;
#88470=LINE ( 'NONE', #67441, #41909 ) ;
#88471=CARTESIAN_POINT ( 'NONE',  ( -23.55512991947090029, -0.7407075233842665973, 4.307968247156982677 ) ) ;
#88472=VERTEX_POINT ( 'NONE', #66347 ) ;
#88473=VECTOR ( 'NONE', #124555, 1000.000000000000000 ) ;
#88474=ORIENTED_EDGE ( 'NONE', *, *, #122029, .F. ) ;
#88476=AXIS2_PLACEMENT_3D ( 'NONE', #17701, #73551, #115567 ) ;
#88478=VERTEX_POINT ( 'NONE', #131589 ) ;
#88480=VERTEX_POINT ( 'NONE', #113198 ) ;
#88481=CARTESIAN_POINT ( 'NONE',  ( 34.47516574401890921, -5.971932658884125722, 4.998110765256833510 ) ) ;
#88482=CARTESIAN_POINT ( 'NONE',  ( 6.328169399223483538, 17.25929247661554200, 4.000000000000000000 ) ) ;
#88483=VECTOR ( 'NONE', #25518, 1000.000000000000000 ) ;
#88484=EDGE_LOOP ( 'NONE', ( #30770, #109392, #37909, #94633 ) ) ;
#88485=CARTESIAN_POINT ( 'NONE',  ( -6.489213562373093325, -27.52281430457059841, 5.000000000000000000 ) ) ;
#88486=PLANE ( 'NONE',  #127498 ) ;
#88487=LINE ( 'NONE', #22466, #81115 ) ;
#88488=PLANE ( 'NONE',  #28078 ) ;
#88492=EDGE_CURVE ( 'NONE', #125073, #59468, #88813, .T. ) ;
#88493=DIRECTION ( 'NONE',  ( -0.7071067811865486830, -0.7071067811865464625, 0.000000000000000000 ) ) ;
#88495=CARTESIAN_POINT ( 'NONE',  ( -34.49999999999975842, 16.46425560840032176, 4.994342998332164107 ) ) ;
#88496=VECTOR ( 'NONE', #82680, 999.9999999999998863 ) ;
#88498=LINE ( 'NONE', #53730, #89400 ) ;
#88499=DIRECTION ( 'NONE',  ( 0.7071067811865487940, 0.7071067811865463515, 0.000000000000000000 ) ) ;
#88500=CARTESIAN_POINT ( 'NONE',  ( -20.47599861414536448, 22.03583458319437582, 4.979811245910088502 ) ) ;
#88501=VERTEX_POINT ( 'NONE', #43871 ) ;
#88502=ORIENTED_EDGE ( 'NONE', *, *, #1854, .F. ) ;
#88504=ORIENTED_EDGE ( 'NONE', *, *, #62999, .T. ) ;
#88509=LINE ( 'NONE', #100089, #48027 ) ;
#88510=EDGE_CURVE ( 'NONE', #76282, #21205, #82740, .T. ) ;
#88512=CARTESIAN_POINT ( 'NONE',  ( -18.48921356237309510, -27.52281430457068367, 5.000000000000000000 ) ) ;
#88514=ORIENTED_EDGE ( 'NONE', *, *, #1356, .T. ) ;
#88515=EDGE_LOOP ( 'NONE', ( #27733, #68210, #87863, #36006 ) ) ;
#88516=VECTOR ( 'NONE', #119593, 1000.000000000000000 ) ;
#88517=PLANE ( 'NONE',  #83205 ) ;
#88518=EDGE_CURVE ( 'NONE', #115411, #77426, #95008, .T. ) ;
#88519=LINE ( 'NONE', #21092, #77918 ) ;
#88520=ORIENTED_EDGE ( 'NONE', *, *, #83163, .T. ) ;
#88521=ORIENTED_EDGE ( 'NONE', *, *, #48946, .F. ) ;
#88523=ORIENTED_EDGE ( 'NONE', *, *, #17531, .T. ) ;
#88524=FACE_OUTER_BOUND ( 'NONE', #117714, .T. ) ;
#88526=CARTESIAN_POINT ( 'NONE',  ( -34.92500000000001137, 4.444556126563251830, 11.73767485154040635 ) ) ;
#88527=AXIS2_PLACEMENT_3D ( 'NONE', #10853, #65300, #42114 ) ;
#88530=ADVANCED_FACE ( 'NONE', ( #92884 ), #136388, .F. ) ;
#88531=DIRECTION ( 'NONE',  ( -0.3543493200069163240, 0.000000000000000000, -0.9351131265310288487 ) ) ;
#88532=ORIENTED_EDGE ( 'NONE', *, *, #45662, .T. ) ;
#88533=ORIENTED_EDGE ( 'NONE', *, *, #134942, .F. ) ;
#88535=AXIS2_PLACEMENT_3D ( 'NONE', #12624, #142453, #99626 ) ;
#88536=VERTEX_POINT ( 'NONE', #82056 ) ;
#88537=VECTOR ( 'NONE', #92056, 1000.000000000000000 ) ;
#88540=AXIS2_PLACEMENT_3D ( 'NONE', #89465, #24224, #121374 ) ;
#88541=EDGE_CURVE ( 'NONE', #132778, #136694, #71163, .T. ) ;
#88542=VECTOR ( 'NONE', #28283, 1000.000000000000000 ) ;
#88543=LINE ( 'NONE', #67513, #123883 ) ;
#88544=DIRECTION ( 'NONE',  ( 0.7071067811865487940, 0.7071067811865463515, -0.000000000000000000 ) ) ;
#88545=ORIENTED_EDGE ( 'NONE', *, *, #37313, .F. ) ;
#88546=LINE ( 'NONE', #130630, #29741 ) ;
#88547=CIRCLE ( 'NONE', #107042, 3.378199999999994319 ) ;
#88548=AXIS2_PLACEMENT_3D ( 'NONE', #42307, #74939, #51025 ) ;
#88549=DIRECTION ( 'NONE',  ( -0.7071067811865487940, 0.7071067811865463515, 0.000000000000000000 ) ) ;
#88550=EDGE_CURVE ( 'NONE', #15815, #103353, #115308, .T. ) ;
#88551=DIRECTION ( 'NONE',  ( 1.000000000000000000, 0.000000000000000000, 0.000000000000000000 ) ) ;
#88552=FACE_BOUND ( 'NONE', #19874, .T. ) ;
#88553=EDGE_CURVE ( 'NONE', #83048, #59118, #92158, .T. ) ;
#88554=ORIENTED_EDGE ( 'NONE', *, *, #27193, .T. ) ;
#88555=CARTESIAN_POINT ( 'NONE',  ( -75.29974487139158157, -27.71228299555258445, 4.000000000000000000 ) ) ;
#88558=ADVANCED_FACE ( 'NONE', ( #28361 ), #106585, .F. ) ;
#88559=ORIENTED_EDGE ( 'NONE', *, *, #47054, .F. ) ;
#88560=CARTESIAN_POINT ( 'NONE',  ( 27.18398860626900060, 28.73617430169806042, 5.000000000000000000 ) ) ;
#88561=ORIENTED_EDGE ( 'NONE', *, *, #15494, .T. ) ;
#88562=ORIENTED_EDGE ( 'NONE', *, *, #36378, .T. ) ;
#88566=VERTEX_POINT ( 'NONE', #61032 ) ;
#88567=EDGE_CURVE ( 'NONE', #106121, #70409, #105185, .T. ) ;
#88568=DIRECTION ( 'NONE',  ( -0.3543493200069162685, -0.000000000000000000, -0.9351131265310288487 ) ) ;
#88569=CARTESIAN_POINT ( 'NONE',  ( -7.499999999999945821, 6.431123077392112641, 4.000000000000000000 ) ) ;
#88570=ORIENTED_EDGE ( 'NONE', *, *, #45424, .T. ) ;
#88572=DIRECTION ( 'NONE',  ( -0.000000000000000000, 0.000000000000000000, 1.000000000000000000 ) ) ;
#88573=EDGE_CURVE ( 'NONE', #31464, #115452, #60291, .T. ) ;
#88574=VECTOR ( 'NONE', #94949, 1000.000000000000227 ) ;
#88575=LINE ( 'NONE', #22544, #82636 ) ;
#88576=LINE ( 'NONE', #110989, #122236 ) ;
#88577=LINE ( 'NONE', #87839, #99075 ) ;
#88580=DIRECTION ( 'NONE',  ( 1.000000000000000000, 0.000000000000000000, 0.000000000000000000 ) ) ;
#88581=ORIENTED_EDGE ( 'NONE', *, *, #8630, .F. ) ;
#88582=ORIENTED_EDGE ( 'NONE', *, *, #84777, .F. ) ;
#88583=ORIENTED_EDGE ( 'NONE', *, *, #118643, .T. ) ;
#88584=VECTOR ( 'NONE', #39097, 1000.000000000000227 ) ;
#88585=LINE ( 'NONE', #77701, #84422 ) ;
#88586=PLANE ( 'NONE',  #9756 ) ;
#88587=VERTEX_POINT ( 'NONE', #5127 ) ;
#88588=ORIENTED_EDGE ( 'NONE', *, *, #88842, .T. ) ;
#88589=DIRECTION ( 'NONE',  ( -1.000000000000000000, 0.000000000000000000, -0.000000000000000000 ) ) ;
#88590=CARTESIAN_POINT ( 'NONE',  ( 5.999999999999957367, -21.41253812416053748, 4.000000000000000000 ) ) ;
#88591=FACE_OUTER_BOUND ( 'NONE', #53236, .T. ) ;
#88592=ORIENTED_EDGE ( 'NONE', *, *, #105833, .F. ) ;
#88593=EDGE_CURVE ( 'NONE', #108717, #17336, #37077, .T. ) ;
#88594=CARTESIAN_POINT ( 'NONE',  ( 32.20666063542130075, 21.75929247661549937, 4.998822639870702744 ) ) ;
#88595=EDGE_CURVE ( 'NONE', #110142, #43034, #117469, .T. ) ;
#88596=DIRECTION ( 'NONE',  ( -0.7071067811865486830, -0.7071067811865464625, 0.000000000000000000 ) ) ;
#88597=EDGE_CURVE ( 'NONE', #134224, #112523, #15292, .T. ) ;
#88600=EDGE_LOOP ( 'NONE', ( #77378, #21130, #100960 ) ) ;
#88602=LINE ( 'NONE', #10289, #7158 ) ;
#88603=VECTOR ( 'NONE', #86738, 1000.000000000000000 ) ;
#88605=FACE_OUTER_BOUND ( 'NONE', #43423, .T. ) ;
#88606=ORIENTED_EDGE ( 'NONE', *, *, #108588, .T. ) ;
#88607=DIRECTION ( 'NONE',  ( 1.000000000000000000, 0.000000000000000000, 0.000000000000000000 ) ) ;
#88608=VECTOR ( 'NONE', #113581, 1000.000000000000227 ) ;
#88609=EDGE_LOOP ( 'NONE', ( #16770, #7733, #84749, #99984 ) ) ;
#88611=EDGE_CURVE ( 'NONE', #81462, #18696, #18144, .T. ) ;
#88613=ORIENTED_EDGE ( 'NONE', *, *, #105418, .T. ) ;
#88614=DIRECTION ( 'NONE',  ( 0.7071067811865487940, 0.7071067811865463515, -0.000000000000000000 ) ) ;
#88615=DIRECTION ( 'NONE',  ( -0.000000000000000000, 0.3543493200069153248, 0.9351131265310292928 ) ) ;
#88617=AXIS2_PLACEMENT_3D ( 'NONE', #53565, #100644, #76022 ) ;
#88618=CARTESIAN_POINT ( 'NONE',  ( 8.999999999999932498, -13.39766691384882513, -10.96608748226467966 ) ) ;
#88619=LINE ( 'NONE', #133540, #90917 ) ;
#88620=ORIENTED_EDGE ( 'NONE', *, *, #87877, .T. ) ;
#88621=CARTESIAN_POINT ( 'NONE',  ( -29.90332935812576309, -2.240707523384260824, 15.26439735382745511 ) ) ;
#88622=FACE_OUTER_BOUND ( 'NONE', #97319, .T. ) ;
#88623=ORIENTED_EDGE ( 'NONE', *, *, #32221, .T. ) ;
#88624=ORIENTED_EDGE ( 'NONE', *, *, #93864, .F. ) ;
#88625=VECTOR ( 'NONE', #99325, 999.9999999999998863 ) ;
#88628=ORIENTED_EDGE ( 'NONE', *, *, #40477, .F. ) ;
#88629=CARTESIAN_POINT ( 'NONE',  ( 29.99999999999979039, -15.41253812416060143, 4.000000000000000000 ) ) ;
#88630=LINE ( 'NONE', #89326, #49217 ) ;
#88631=VERTEX_POINT ( 'NONE', #6541 ) ;
#88632=ADVANCED_FACE ( 'NONE', ( #125537 ), #26218, .F. ) ;
#88633=FACE_OUTER_BOUND ( 'NONE', #120262, .T. ) ;
#88634=CARTESIAN_POINT ( 'NONE',  ( 48.18398860626899705, 28.73617430169820608, 5.000000000000000000 ) ) ;
#88635=VECTOR ( 'NONE', #44416, 1000.000000000000000 ) ;
#88636=VECTOR ( 'NONE', #49136, 1000.000000000000227 ) ;
#88640=AXIS2_PLACEMENT_3D ( 'NONE', #120456, #123391, #87161 ) ;
#88641=VECTOR ( 'NONE', #49709, 999.9999999999998863 ) ;
#88642=EDGE_LOOP ( 'NONE', ( #65964, #138158, #31534, #79 ) ) ;
#88643=ORIENTED_EDGE ( 'NONE', *, *, #29222, .T. ) ;
#88645=EDGE_LOOP ( 'NONE', ( #103062, #19529, #105781, #16382 ) ) ;
#88646=ORIENTED_EDGE ( 'NONE', *, *, #84922, .T. ) ;
#88648=VECTOR ( 'NONE', #38908, 1000.000000000000000 ) ;
#88649=DIRECTION ( 'NONE',  ( -0.7071067811865486830, -0.7071067811865464625, 0.000000000000000000 ) ) ;
#88650=LINE ( 'NONE', #69040, #46277 ) ;
#88651=ORIENTED_EDGE ( 'NONE', *, *, #2546, .F. ) ;
#88652=CARTESIAN_POINT ( 'NONE',  ( 1.499999999999990896, -20.56887692260760048, 4.000000000000000000 ) ) ;
#88654=EDGE_CURVE ( 'NONE', #85221, #51427, #43508, .T. ) ;
#88655=CARTESIAN_POINT ( 'NONE',  ( 7.499999999999956479, 0.05218569542916884352, 5.000000000000000000 ) ) ;
#88656=CARTESIAN_POINT ( 'NONE',  ( 35.99451991528749772, 28.92564299267963079, 4.000000000000000000 ) ) ;
#88658=EDGE_CURVE ( 'NONE', #100160, #6566, #18890, .T. ) ;
#88660=DIRECTION ( 'NONE',  ( 1.000000000000000000, 0.000000000000000000, 0.000000000000000000 ) ) ;
#88661=DIRECTION ( 'NONE',  ( -0.3543493200069162685, -0.000000000000000000, -0.9351131265310288487 ) ) ;
#88662=LINE ( 'NONE', #56050, #112047 ) ;
#88663=CARTESIAN_POINT ( 'NONE',  ( -36.18398860626899705, 28.73617430169812437, 5.000000000000000000 ) ) ;
#88664=DIRECTION ( 'NONE',  ( 0.7071067811865487940, -0.7071067811865463515, 0.000000000000000000 ) ) ;
#88665=CARTESIAN_POINT ( 'NONE',  ( 29.99999999999979750, 20.96639925780204905, 5.000000000000000000 ) ) ;
#88666=EDGE_CURVE ( 'NONE', #64166, #131176, #21760, .T. ) ;
#88668=EDGE_CURVE ( 'NONE', #18279, #38139, #76145, .T. ) ;
#88669=DIRECTION ( 'NONE',  ( -0.6830127018922181881, 0.6830127018922202975, -0.2588190451025214056 ) ) ;
#88670=AXIS2_PLACEMENT_3D ( 'NONE', #105361, #138732, #15470 ) ;
#88671=LINE ( 'NONE', #13918, #115531 ) ;
#88672=ORIENTED_EDGE ( 'NONE', *, *, #128443, .T. ) ;
#88675=EDGE_CURVE ( 'NONE', #50352, #39505, #109479, .T. ) ;
#88676=CARTESIAN_POINT ( 'NONE',  ( -5.510786437626906675, -27.52281430457051314, 5.000000000000000000 ) ) ;
#88677=DIRECTION ( 'NONE',  ( 0.7071067811865487940, 0.7071067811865463515, 0.000000000000000000 ) ) ;
#88678=EDGE_LOOP ( 'NONE', ( #115580, #139826, #36897, #48989 ) ) ;
#88679=DIRECTION ( 'NONE',  ( 0.6830127018922180770, -0.6830127018922204085, -0.2588190451025213501 ) ) ;
#88680=CARTESIAN_POINT ( 'NONE',  ( -56.99451991528749062, 28.92564299267978001, 4.000000000000000000 ) ) ;
#88681=EDGE_CURVE ( 'NONE', #44075, #76243, #98591, .T. ) ;
#88686=ORIENTED_EDGE ( 'NONE', *, *, #81991, .F. ) ;
#88687=VERTEX_POINT ( 'NONE', #84868 ) ;
#88688=PLANE ( 'NONE',  #79710 ) ;
#88689=EDGE_CURVE ( 'NONE', #28531, #60511, #142822, .T. ) ;
#88692=CARTESIAN_POINT ( 'NONE',  ( -3.299744871391591339, -27.71228299555208352, 4.000000000000000000 ) ) ;
#88693=EDGE_LOOP ( 'NONE', ( #92818, #101371, #95339, #75347 ) ) ;
#88694=CARTESIAN_POINT ( 'NONE',  ( 65.99451991528749772, 28.92564299267984396, 4.000000000000000000 ) ) ;
#88695=ORIENTED_EDGE ( 'NONE', *, *, #138597, .T. ) ;
#88697=LINE ( 'NONE', #25551, #43884 ) ;
#88700=EDGE_CURVE ( 'NONE', #18390, #61904, #131230, .T. ) ;
#88702=CARTESIAN_POINT ( 'NONE',  ( -24.48921356237309510, -27.52281430457072631, 5.000000000000000000 ) ) ;
#88704=VERTEX_POINT ( 'NONE', #85566 ) ;
#88705=( BOUNDED_CURVE ( )  B_SPLINE_CURVE ( 3, ( #68730, #67292, #12874, #79644 ),
 .UNSPECIFIED., .F., .T. ) 
 B_SPLINE_CURVE_WITH_KNOTS ( ( 4, 4 ),
 ( 5.920967161967926273, 7.341195215986655143 ),
 .UNSPECIFIED. ) 
 CURVE ( )  GEOMETRIC_REPRESENTATION_ITEM ( )  RATIONAL_B_SPLINE_CURVE ( ( 1.000000000000000000, 0.8388583629366573868, 0.8388583629366573868, 1.000000000000000000 ) ) 
 REPRESENTATION_ITEM ( '' )  );
#88709=VECTOR ( 'NONE', #58978, 999.9999999999998863 ) ;
#88710=EDGE_CURVE ( 'NONE', #8502, #27215, #31920, .T. ) ;
#88711=DIRECTION ( 'NONE',  ( -0.6830127018922180770, -0.6830127018922204085, -0.2588190451025213501 ) ) ;
#88712=CARTESIAN_POINT ( 'NONE',  ( 34.49999999999976552, 7.464255608400424791, 4.994342998332163219 ) ) ;
#88713=VERTEX_POINT ( 'NONE', #97127 ) ;
#88714=EDGE_LOOP ( 'NONE', ( #127760, #96909, #76046, #100186 ) ) ;
#88715=VECTOR ( 'NONE', #45716, 1000.000000000000000 ) ;
#88716=DIRECTION ( 'NONE',  ( 0.6830127018922181881, 0.6830127018922202975, -0.2588190451025214056 ) ) ;
#88717=ORIENTED_EDGE ( 'NONE', *, *, #91138, .F. ) ;
#88719=DIRECTION ( 'NONE',  ( 1.000000000000000000, 0.000000000000000000, 0.000000000000000000 ) ) ;
#88720=VERTEX_POINT ( 'NONE', #142131 ) ;
#88721=EDGE_CURVE ( 'NONE', #61026, #79521, #36077, .T. ) ;
#88722=CARTESIAN_POINT ( 'NONE',  ( -24.18398860626899705, 28.73617430169804265, 5.000000000000000000 ) ) ;
#88723=LINE ( 'NONE', #56833, #43344 ) ;
#88725=EDGE_CURVE ( 'NONE', #6025, #16532, #76886, .T. ) ;
#88726=DIRECTION ( 'NONE',  ( -0.6830127018922180770, -0.6830127018922204085, -0.2588190451025213501 ) ) ;
#88727=FACE_BOUND ( 'NONE', #82988, .T. ) ;
#88729=DIRECTION ( 'NONE',  ( -0.7071067811865486830, -0.7071067811865464625, 0.000000000000000000 ) ) ;
#88730=CARTESIAN_POINT ( 'NONE',  ( 48.29974487139158867, -27.71228299555239971, 4.000000000000000000 ) ) ;
#88732=CARTESIAN_POINT ( 'NONE',  ( 28.40832548098983423, -0.7407075233842701500, 14.76736230305387210 ) ) ;
#88734=ORIENTED_EDGE ( 'NONE', *, *, #126878, .F. ) ;
#88736=EDGE_LOOP ( 'NONE', ( #52068, #24550, #42940, #19421 ) ) ;
#88737=ORIENTED_EDGE ( 'NONE', *, *, #29236, .T. ) ;
#88739=VERTEX_POINT ( 'NONE', #21025 ) ;
#88740=DIRECTION ( 'NONE',  ( -0.000000000000000000, -0.3543493200069152693, 0.9351131265310292928 ) ) ;
#88742=DIRECTION ( 'NONE',  ( 0.7071067811865487940, 0.7071067811865463515, 0.000000000000000000 ) ) ;
#88743=ORIENTED_EDGE ( 'NONE', *, *, #127966, .F. ) ;
#88745=VECTOR ( 'NONE', #138535, 999.9999999999998863 ) ;
#88746=EDGE_CURVE ( 'NONE', #136709, #33315, #95741, .T. ) ;
#88748=CARTESIAN_POINT ( 'NONE',  ( 3.469446951953614189E-15, -3.485240976185081330, -4.108735105802396426 ) ) ;
#88749=DIRECTION ( 'NONE',  ( -0.7071067811865486830, -0.7071067811865464625, 0.000000000000000000 ) ) ;
#88750=DIRECTION ( 'NONE',  ( 0.7071067811865486830, -0.7071067811865464625, -0.000000000000000000 ) ) ;
#88751=CARTESIAN_POINT ( 'NONE',  ( -33.32816939922329880, -12.74070752338415602, 4.000000000000000000 ) ) ;
#88752=LINE ( 'NONE', #20598, #117986 ) ;
#88754=VECTOR ( 'NONE', #928, 1000.000000000000227 ) ;
#88756=CARTESIAN_POINT ( 'NONE',  ( 10.49999999999992362, 18.43112307739199451, 4.000000000000000000 ) ) ;
#88757=ORIENTED_EDGE ( 'NONE', *, *, #121376, .F. ) ;
#88758=PLANE ( 'NONE',  #40344 ) ;
#88759=VECTOR ( 'NONE', #91427, 1000.000000000000000 ) ;
#88760=CARTESIAN_POINT ( 'NONE',  ( 7.110173228882053387, -22.22500000000000497, 4.785647885939352086 ) ) ;
#88762=ORIENTED_EDGE ( 'NONE', *, *, #13865, .F. ) ;
#88763=FACE_OUTER_BOUND ( 'NONE', #24376, .T. ) ;
#88764=CARTESIAN_POINT ( 'NONE',  ( 23.99451991528749062, 28.92564299267954908, 4.000000000000000000 ) ) ;
#88765=ORIENTED_EDGE ( 'NONE', *, *, #117526, .F. ) ;
#88766=DIRECTION ( 'NONE',  ( -0.7071067811865486830, -0.7071067811865464625, 0.000000000000000000 ) ) ;
#88767=ADVANCED_FACE ( 'NONE', ( #29757 ), #74002, .T. ) ;
#88768=CARTESIAN_POINT ( 'NONE',  ( -24.18398860626899705, 28.73617430169804265, 5.000000000000000000 ) ) ;
#88769=VECTOR ( 'NONE', #84200, 1000.000000000000000 ) ;
#88772=EDGE_LOOP ( 'NONE', ( #109660, #94961, #112334, #64476 ) ) ;
#88774=FACE_OUTER_BOUND ( 'NONE', #74312, .T. ) ;
#88775=CARTESIAN_POINT ( 'NONE',  ( -18.18398860626898994, 28.73617430169800002, 5.000000000000000000 ) ) ;
#88776=DIRECTION ( 'NONE',  ( -0.7071067811865487940, 0.7071067811865463515, -0.000000000000000000 ) ) ;
#88777=ORIENTED_EDGE ( 'NONE', *, *, #5824, .F. ) ;
#88778=VERTEX_POINT ( 'NONE', #7996 ) ;
#88780=CARTESIAN_POINT ( 'NONE',  ( 32.99999999999977973, -19.44781430457062754, 5.000000000000000000 ) ) ;
#88781=VECTOR ( 'NONE', #35995, 1000.000000000000000 ) ;
#88785=DIRECTION ( 'NONE',  ( 0.7071067811865487940, -0.7071067811865463515, 0.000000000000000000 ) ) ;
#88786=ORIENTED_EDGE ( 'NONE', *, *, #134937, .T. ) ;
#88787=VECTOR ( 'NONE', #74332, 1000.000000000000227 ) ;
#88788=CARTESIAN_POINT ( 'NONE',  ( -71.99451991528749772, 28.92564299267988304, 4.000000000000000000 ) ) ;
#88789=CARTESIAN_POINT ( 'NONE',  ( 8.111623618947536585, 9.759292476615614831, 17.35367589129210941 ) ) ;
#88790=CARTESIAN_POINT ( 'NONE',  ( -10.82816939922344801, 18.75929247661552779, 4.000000000000000000 ) ) ;
#88792=FACE_OUTER_BOUND ( 'NONE', #38100, .T. ) ;
#88793=VECTOR ( 'NONE', #1871, 999.9999999999998863 ) ;
#88794=CARTESIAN_POINT ( 'NONE',  ( -14.99451991528749595, 28.92564299267948513, 4.000000000000000000 ) ) ;
#88795=CARTESIAN_POINT ( 'NONE',  ( -12.48921356237309155, -27.52281430457064104, 5.000000000000000000 ) ) ;
#88796=ORIENTED_EDGE ( 'NONE', *, *, #142292, .F. ) ;
#88797=PLANE ( 'NONE',  #69814 ) ;
#88800=CARTESIAN_POINT ( 'NONE',  ( 9.706123077391888287, 22.22500000000000142, 4.000000000000000000 ) ) ;
#88801=VECTOR ( 'NONE', #124378, 1000.000000000000227 ) ;
#88803=FACE_OUTER_BOUND ( 'NONE', #41096, .T. ) ;
#88804=VECTOR ( 'NONE', #108342, 1000.000000000000000 ) ;
#88805=ORIENTED_EDGE ( 'NONE', *, *, #140990, .F. ) ;
#88806=CARTESIAN_POINT ( 'NONE',  ( 15.32816939922342847, 17.25929247661554200, 4.000000000000000000 ) ) ;
#88807=DIRECTION ( 'NONE',  ( 0.7071067811865487940, 0.7071067811865463515, -0.000000000000000000 ) ) ;
#88808=DIRECTION ( 'NONE',  ( -0.7071067811865486830, -0.7071067811865464625, 0.000000000000000000 ) ) ;
#88809=ORIENTED_EDGE ( 'NONE', *, *, #98796, .F. ) ;
#88810=DIRECTION ( 'NONE',  ( 1.000000000000000000, 0.000000000000000000, 0.000000000000000000 ) ) ;
#88812=VECTOR ( 'NONE', #65876, 1000.000000000000000 ) ;
#88813=LINE ( 'NONE', #98934, #42836 ) ;
#88814=DIRECTION ( 'NONE',  ( 0.7071067811865486830, -0.7071067811865464625, -0.000000000000000000 ) ) ;
#88816=DIRECTION ( 'NONE',  ( -0.7071067811865486830, -0.7071067811865464625, 0.000000000000000000 ) ) ;
#88817=CARTESIAN_POINT ( 'NONE',  ( -51.29974487139158867, -27.71228299555242103, 4.000000000000000000 ) ) ;
#88819=LINE ( 'NONE', #86673, #48800 ) ;
#88820=ORIENTED_EDGE ( 'NONE', *, *, #29047, .F. ) ;
#88821=CARTESIAN_POINT ( 'NONE',  ( -4.499999999999962697, -6.839392718269134974, -8.480912228396073615 ) ) ;
#88822=ADVANCED_FACE ( 'NONE', ( #20303 ), #96420, .T. ) ;
#88823=EDGE_LOOP ( 'NONE', ( #9578, #115376, #138224, #39895 ) ) ;
#88824=VECTOR ( 'NONE', #60634, 1000.000000000000227 ) ;
#88825=DIRECTION ( 'NONE',  ( 0.7071067811865487940, 0.7071067811865463515, -0.000000000000000000 ) ) ;
#88826=DIRECTION ( 'NONE',  ( 0.7071067811865487940, 0.7071067811865463515, -0.000000000000000000 ) ) ;
#88827=CARTESIAN_POINT ( 'NONE',  ( -26.20710678118635428, -20.24070752338407786, 5.000000000000000000 ) ) ;
#88828=LINE ( 'NONE', #43888, #65066 ) ;
#88829=DIRECTION ( 'NONE',  ( 1.000000000000000000, 0.000000000000000000, 0.000000000000000000 ) ) ;
#88830=LINE ( 'NONE', #1054, #138020 ) ;
#88832=ADVANCED_FACE ( 'NONE', ( #99286 ), #134098, .F. ) ;
#88834=AXIS2_PLACEMENT_3D ( 'NONE', #15525, #114848, #27867 ) ;
#88835=ORIENTED_EDGE ( 'NONE', *, *, #63153, .F. ) ;
#88836=FACE_OUTER_BOUND ( 'NONE', #17243, .T. ) ;
#88837=PLANE ( 'NONE',  #60637 ) ;
#88838=DIRECTION ( 'NONE',  ( 0.7071067811865487940, -0.7071067811865463515, 0.000000000000000000 ) ) ;
#88839=CARTESIAN_POINT ( 'NONE',  ( 0.000000000000000000, -21.72500000000000142, 4.500000000000000888 ) ) ;
#88840=EDGE_CURVE ( 'NONE', #39920, #70502, #2844, .T. ) ;
#88842=EDGE_CURVE ( 'NONE', #32743, #111517, #90593, .T. ) ;
#88844=AXIS2_PLACEMENT_3D ( 'NONE', #101933, #35987, #122979 ) ;
#88845=CARTESIAN_POINT ( 'NONE',  ( -10.49999999999992895, -19.91253812416055169, 4.000000000000000000 ) ) ;
#88846=VERTEX_POINT ( 'NONE', #23908 ) ;
#88847=ADVANCED_FACE ( 'NONE', ( #121759 ), #33388, .F. ) ;
#88849=FACE_OUTER_BOUND ( 'NONE', #89260, .T. ) ;
#88850=EDGE_CURVE ( 'NONE', #39702, #94617, #77590, .T. ) ;
#88851=CARTESIAN_POINT ( 'NONE',  ( -34.42500000000001137, -1.458600742197974087, 5.000000000000000000 ) ) ;
#88852=CARTESIAN_POINT ( 'NONE',  ( -22.49999999999985434, 13.56627193232213102, -10.57019076586073680 ) ) ;
#88853=EDGE_CURVE ( 'NONE', #105060, #28681, #44990, .T. ) ;
#88854=VERTEX_POINT ( 'NONE', #12294 ) ;
#88856=DIRECTION ( 'NONE',  ( -0.7071067811865486830, -0.7071067811865464625, 0.000000000000000000 ) ) ;
#88857=EDGE_CURVE ( 'NONE', #54435, #8757, #68170, .T. ) ;
#88858=ORIENTED_EDGE ( 'NONE', *, *, #22647, .T. ) ;
#88859=FACE_OUTER_BOUND ( 'NONE', #27564, .T. ) ;
#88861=DIRECTION ( 'NONE',  ( -0.3543493200069162685, -0.000000000000000000, -0.9351131265310288487 ) ) ;
#88862=VERTEX_POINT ( 'NONE', #124633 ) ;
#88863=DIRECTION ( 'NONE',  ( 0.7071067811865486830, -0.7071067811865464625, -0.000000000000000000 ) ) ;
#88864=DIRECTION ( 'NONE',  ( 0.7071067811865487940, 0.7071067811865463515, -0.000000000000000000 ) ) ;
#88865=ADVANCED_FACE ( 'NONE', ( #23149 ), #110169, .F. ) ;
#88866=CARTESIAN_POINT ( 'NONE',  ( 20.86500426248364803, 3.759292476615681888, 15.36553568819721072 ) ) ;
#88867=LINE ( 'NONE', #131647, #131949 ) ;
#88868=CARTESIAN_POINT ( 'NONE',  ( 6.792893218813416567, 0.7592924766157104211, 5.000000000000000000 ) ) ;
#88869=ORIENTED_EDGE ( 'NONE', *, *, #140053, .T. ) ;
#88870=CARTESIAN_POINT ( 'NONE',  ( 31.49999999999977973, 9.431123077392099319, 4.000000000000000000 ) ) ;
#88871=CARTESIAN_POINT ( 'NONE',  ( 23.99999999999983302, -16.06887692260764666, 4.000000000000000000 ) ) ;
#88872=CYLINDRICAL_SURFACE ( 'NONE', #30886, 0.5000000000000004441 ) ;
#88873=AXIS2_PLACEMENT_3D ( 'NONE', #26669, #104936, #115773 ) ;
#88874=EDGE_CURVE ( 'NONE', #31789, #2906, #11555, .T. ) ;
#88875=LINE ( 'NONE', #31621, #2083 ) ;
#88876=ORIENTED_EDGE ( 'NONE', *, *, #5420, .F. ) ;
#88877=EDGE_LOOP ( 'NONE', ( #124546, #61693, #40083, #46936 ) ) ;
#88879=AXIS2_PLACEMENT_3D ( 'NONE', #81157, #70315, #135538 ) ;
#88880=VERTEX_POINT ( 'NONE', #143530 ) ;
#88881=LINE ( 'NONE', #133108, #79994 ) ;
#88882=LINE ( 'NONE', #22148, #7034 ) ;
#88883=DIRECTION ( 'NONE',  ( 0.7071067811865487940, 0.7071067811865463515, -0.000000000000000000 ) ) ;
#88884=LINE ( 'NONE', #57691, #91975 ) ;
#88885=DIRECTION ( 'NONE',  ( 0.7071067811865486830, -0.7071067811865464625, -0.000000000000000000 ) ) ;
#88886=VERTEX_POINT ( 'NONE', #1395 ) ;
#88887=ORIENTED_EDGE ( 'NONE', *, *, #14908, .T. ) ;
#88888=CARTESIAN_POINT ( 'NONE',  ( 39.18398860626899705, 28.73617430169814568, 5.000000000000000000 ) ) ;
#88890=VECTOR ( 'NONE', #117603, 1000.000000000000227 ) ;
#88891=EDGE_CURVE ( 'NONE', #751, #97422, #68857, .T. ) ;
#88893=AXIS2_PLACEMENT_3D ( 'NONE', #119065, #54558, #10298 ) ;
#88895=ADVANCED_FACE ( 'NONE', ( #133390 ), #34078, .F. ) ;
#88896=PLANE ( 'NONE',  #22500 ) ;
#88897=LINE ( 'NONE', #133120, #134990 ) ;
#88899=ORIENTED_EDGE ( 'NONE', *, *, #42760, .T. ) ;
#88900=VECTOR ( 'NONE', #98057, 1000.000000000000000 ) ;
#88902=FACE_BOUND ( 'NONE', #121302, .T. ) ;
#88904=FACE_OUTER_BOUND ( 'NONE', #103313, .T. ) ;
#88906=LINE ( 'NONE', #78018, #36501 ) ;
#88907=VECTOR ( 'NONE', #46943, 1000.000000000000000 ) ;
#88908=VECTOR ( 'NONE', #80381, 1000.000000000000000 ) ;
#88909=CARTESIAN_POINT ( 'NONE',  ( -32.99451991528749062, 28.92564299267960948, 4.000000000000000000 ) ) ;
#88910=ORIENTED_EDGE ( 'NONE', *, *, #135209, .T. ) ;
#88911=VECTOR ( 'NONE', #85506, 999.9999999999998863 ) ;
#88912=VERTEX_POINT ( 'NONE', #123941 ) ;
#88914=EDGE_LOOP ( 'NONE', ( #133200, #61544, #69631, #3673 ) ) ;
#88915=EDGE_CURVE ( 'NONE', #41910, #14576, #12997, .T. ) ;
#88916=CARTESIAN_POINT ( 'NONE',  ( -27.48921356237309155, -27.52281430457074762, 5.000000000000000000 ) ) ;
#88917=VERTEX_POINT ( 'NONE', #47142 ) ;
#88918=VECTOR ( 'NONE', #54081, 1000.000000000000000 ) ;
#88919=PLANE ( 'NONE',  #70219 ) ;
#88920=FACE_OUTER_BOUND ( 'NONE', #16085, .T. ) ;
#88921=VECTOR ( 'NONE', #43101, 1000.000000000000000 ) ;
#88923=VERTEX_POINT ( 'NONE', #35529 ) ;
#88924=PLANE ( 'NONE',  #85412 ) ;
#88925=PLANE ( 'NONE',  #100528 ) ;
#88926=EDGE_CURVE ( 'NONE', #31980, #94995, #79761, .T. ) ;
#88927=DIRECTION ( 'NONE',  ( 0.000000000000000000, 1.000000000000000000, 0.000000000000000000 ) ) ;
#88928=DIRECTION ( 'NONE',  ( -0.000000000000000000, -0.3543493200069152693, 0.9351131265310292928 ) ) ;
#88929=DIRECTION ( 'NONE',  ( 0.7071067811865487940, -0.7071067811865463515, 0.000000000000000000 ) ) ;
#88931=VECTOR ( 'NONE', #140468, 1000.000000000000000 ) ;
#88932=CARTESIAN_POINT ( 'NONE',  ( -7.499999999999944045, 1.466399257802248446, 5.000000000000000000 ) ) ;
#88933=ORIENTED_EDGE ( 'NONE', *, *, #86571, .F. ) ;
#88934=CARTESIAN_POINT ( 'NONE',  ( -8.292893218813398803, 14.25929247661557575, 5.000000000000000000 ) ) ;
#88935=FACE_OUTER_BOUND ( 'NONE', #126028, .T. ) ;
#88936=ORIENTED_EDGE ( 'NONE', *, *, #43640, .F. ) ;
#88937=ORIENTED_EDGE ( 'NONE', *, *, #64578, .F. ) ;
#88938=ORIENTED_EDGE ( 'NONE', *, *, #104721, .T. ) ;
#88940=ORIENTED_EDGE ( 'NONE', *, *, #11537, .T. ) ;
#88941=PLANE ( 'NONE',  #90543 ) ;
#88942=AXIS2_PLACEMENT_3D ( 'NONE', #44949, #8129, #121015 ) ;
#88944=FACE_OUTER_BOUND ( 'NONE', #19208, .T. ) ;
#88946=ORIENTED_EDGE ( 'NONE', *, *, #33298, .T. ) ;
#88947=CARTESIAN_POINT ( 'NONE',  ( -34.42500000000001137, -22.22500000000000142, 5.000000000000000000 ) ) ;
#88948=DIRECTION ( 'NONE',  ( -0.7071067811865486830, -0.7071067811865464625, 0.000000000000000000 ) ) ;
#88949=ORIENTED_EDGE ( 'NONE', *, *, #86027, .F. ) ;
#88950=VECTOR ( 'NONE', #50226, 1000.000000000000000 ) ;
#88951=EDGE_CURVE ( 'NONE', #132937, #104393, #91321, .T. ) ;
#88952=CARTESIAN_POINT ( 'NONE',  ( 12.79289321881337216, 12.75929247661559174, 5.000000000000000000 ) ) ;
#88953=DIRECTION ( 'NONE',  ( 0.6830127018922181881, 0.6830127018922202975, -0.2588190451025214056 ) ) ;
#88954=EDGE_LOOP ( 'NONE', ( #100198, #115776, #75324, #122789 ) ) ;
#88955=ADVANCED_FACE ( 'NONE', ( #91997 ), #49246, .F. ) ;
#88956=DIRECTION ( 'NONE',  ( 0.6830127018922180770, -0.6830127018922204085, -0.2588190451025213501 ) ) ;
#88957=VERTEX_POINT ( 'NONE', #113758 ) ;
#88958=ORIENTED_EDGE ( 'NONE', *, *, #96512, .T. ) ;
#88959=ORIENTED_EDGE ( 'NONE', *, *, #106308, .F. ) ;
#88961=CARTESIAN_POINT ( 'NONE',  ( 78.48921356237309510, -27.52281430457109934, 5.000000000000000000 ) ) ;
#88964=ORIENTED_EDGE ( 'NONE', *, *, #57735, .T. ) ;
#88965=CARTESIAN_POINT ( 'NONE',  ( 20.48334561358940675, 22.22500000000000142, 4.500000000000000888 ) ) ;
#88967=VECTOR ( 'NONE', #67160, 999.9999999999998863 ) ;
#88968=VECTOR ( 'NONE', #53904, 1000.000000000000000 ) ;
#88971=DIRECTION ( 'NONE',  ( -0.7071067811865486830, 0.7071067811865464625, 0.000000000000000000 ) ) ;
#88972=DIRECTION ( 'NONE',  ( -0.7071067811865487940, 0.7071067811865463515, -0.000000000000000000 ) ) ;
#88975=ORIENTED_EDGE ( 'NONE', *, *, #62281, .T. ) ;
#88976=ORIENTED_EDGE ( 'NONE', *, *, #141747, .F. ) ;
#88977=LINE ( 'NONE', #44032, #101925 ) ;
#88978=FACE_OUTER_BOUND ( 'NONE', #39765, .T. ) ;
#88979=CARTESIAN_POINT ( 'NONE',  ( 36.48921356237310221, -27.52281430457080802, 5.000000000000000000 ) ) ;
#88980=LINE ( 'NONE', #21567, #87618 ) ;
#88981=LINE ( 'NONE', #112157, #101606 ) ;
#88982=VECTOR ( 'NONE', #33370, 1000.000000000000000 ) ;
#88983=CARTESIAN_POINT ( 'NONE',  ( 1.499999999999994449, 9.052185695429081136, 5.000000000000000000 ) ) ;
#88984=CARTESIAN_POINT ( 'NONE',  ( -9.489213562373095101, -27.52281430457062328, 5.000000000000000000 ) ) ;
#88985=DIRECTION ( 'NONE',  ( -1.000000000000000000, 7.120242111146219159E-15, 0.000000000000000000 ) ) ;
#88987=CARTESIAN_POINT ( 'NONE',  ( -23.99999999999983302, 7.931123077392102871, 4.000000000000000000 ) ) ;
#88988=VERTEX_POINT ( 'NONE', #81148 ) ;
#88992=DIRECTION ( 'NONE',  ( 0.7071067811865486830, -0.7071067811865464625, -0.000000000000000000 ) ) ;
#88994=ORIENTED_EDGE ( 'NONE', *, *, #107205, .T. ) ;
#88995=VECTOR ( 'NONE', #14234, 1000.000000000000000 ) ;
#88996=LINE ( 'NONE', #57090, #4619 ) ;
#88997=CARTESIAN_POINT ( 'NONE',  ( 26.24139925780185578, 21.72500000000000142, 5.000000000000000000 ) ) ;
#88998=ADVANCED_FACE ( 'NONE', ( #70995 ), #61556, .F. ) ;
#88999=ORIENTED_EDGE ( 'NONE', *, *, #43027, .F. ) ;
#89000=PLANE ( 'NONE',  #85535 ) ;
#89001=ORIENTED_EDGE ( 'NONE', *, *, #18502, .F. ) ;
#89003=EDGE_LOOP ( 'NONE', ( #52566, #37880, #80274, #83147 ) ) ;
#89004=AXIS2_PLACEMENT_3D ( 'NONE', #41313, #46924, #48286 ) ;
#89005=CARTESIAN_POINT ( 'NONE',  ( -8.345055162546129779, 5.259292476615662792, 12.77922209995892011 ) ) ;
#89007=EDGE_CURVE ( 'NONE', #43696, #116862, #102897, .T. ) ;
#89009=VECTOR ( 'NONE', #19045, 1000.000000000000000 ) ;
#89010=VECTOR ( 'NONE', #85369, 1000.000000000000227 ) ;
#89011=DIRECTION ( 'NONE',  ( -0.7071067811865486830, -0.7071067811865464625, 0.000000000000000000 ) ) ;
#89012=EDGE_CURVE ( 'NONE', #8228, #109090, #58729, .T. ) ;
#89013=CARTESIAN_POINT ( 'NONE',  ( 2.999999999999975131, 9.631307414974328296, -9.079085613539536581 ) ) ;
#89014=LINE ( 'NONE', #112877, #42618 ) ;
#89016=LINE ( 'NONE', #24442, #122514 ) ;
#89018=CARTESIAN_POINT ( 'NONE',  ( -2.510786437626908008, -27.52281430457053446, 5.000000000000000000 ) ) ;
#89020=FACE_OUTER_BOUND ( 'NONE', #25217, .T. ) ;
#89021=EDGE_CURVE ( 'NONE', #88053, #77065, #116612, .T. ) ;
#89022=VERTEX_POINT ( 'NONE', #49948 ) ;
#89023=ORIENTED_EDGE ( 'NONE', *, *, #106279, .F. ) ;
#89024=CARTESIAN_POINT ( 'NONE',  ( 22.82816939922337696, 12.75929247661558996, 4.000000000000000000 ) ) ;
#89025=ORIENTED_EDGE ( 'NONE', *, *, #106209, .T. ) ;
#89026=EDGE_CURVE ( 'NONE', #91989, #70462, #60855, .T. ) ;
#89028=CARTESIAN_POINT ( 'NONE',  ( -3.328169399223507519, -12.74070752338415602, 4.000000000000000000 ) ) ;
#89029=LINE ( 'NONE', #135393, #16187 ) ;
#89030=LINE ( 'NONE', #58580, #40038 ) ;
#89031=LINE ( 'NONE', #67265, #135861 ) ;
#89034=CYLINDRICAL_SURFACE ( 'NONE', #106676, 0.5000000000000004441 ) ;
#89035=EDGE_CURVE ( 'NONE', #98425, #34748, #127487, .T. ) ;
#89037=ADVANCED_FACE ( 'NONE', ( #104281 ), #136937, .F. ) ;
#89038=LINE ( 'NONE', #54973, #67054 ) ;
#89039=CARTESIAN_POINT ( 'NONE',  ( -54.48921356237310221, -27.52281430457093236, 5.000000000000000000 ) ) ;
#89040=CARTESIAN_POINT ( 'NONE',  ( -4.499999999999972466, 19.39370406404966829, 1.459788787078212025 ) ) ;
#89043=DIRECTION ( 'NONE',  ( 0.7071067811865486830, -0.7071067811865464625, -0.000000000000000000 ) ) ;
#89044=LINE ( 'NONE', #78884, #68829 ) ;
#89045=EDGE_CURVE ( 'NONE', #10796, #133726, #93439, .T. ) ;
#89046=CARTESIAN_POINT ( 'NONE',  ( 24.48921356237309510, -27.52281430457072631, 5.000000000000000000 ) ) ;
#89047=ORIENTED_EDGE ( 'NONE', *, *, #49381, .F. ) ;
#89048=VERTEX_POINT ( 'NONE', #103573 ) ;
#89052=LINE ( 'NONE', #35401, #78758 ) ;
#89053=DIRECTION ( 'NONE',  ( -0.000000000000000000, -0.3543493200069152693, 0.9351131265310292928 ) ) ;
#89054=DIRECTION ( 'NONE',  ( 1.000000000000000000, 0.000000000000000000, 0.000000000000000000 ) ) ;
#89055=ORIENTED_EDGE ( 'NONE', *, *, #53978, .F. ) ;
#89056=LINE ( 'NONE', #122348, #118480 ) ;
#89057=CARTESIAN_POINT ( 'NONE',  ( -32.29289321881321939, 11.25929247661559884, 5.000000000000000000 ) ) ;
#89060=VERTEX_POINT ( 'NONE', #94129 ) ;
#89061=LINE ( 'NONE', #45575, #74407 ) ;
#89062=EDGE_CURVE ( 'NONE', #11322, #13287, #136216, .T. ) ;
#89063=CARTESIAN_POINT ( 'NONE',  ( 34.49999999999975842, 12.05432934483081908, 4.994342998332162331 ) ) ;
#89064=ORIENTED_EDGE ( 'NONE', *, *, #61082, .T. ) ;
#89065=ORIENTED_EDGE ( 'NONE', *, *, #55260, .F. ) ;
#89066=EDGE_LOOP ( 'NONE', ( #135853, #58714, #57937, #5105 ) ) ;
#89067=LINE ( 'NONE', #133287, #51483 ) ;
#89068=DIRECTION ( 'NONE',  ( 1.000000000000000000, -0.000000000000000000, 0.000000000000000000 ) ) ;
#89070=LINE ( 'NONE', #67315, #103525 ) ;
#89071=EDGE_CURVE ( 'NONE', #107544, #99130, #39798, .T. ) ;
#89073=DIRECTION ( 'NONE',  ( 0.7071067811865486830, -0.7071067811865464625, -0.000000000000000000 ) ) ;
#89074=AXIS2_PLACEMENT_3D ( 'NONE', #52966, #9446, #42851 ) ;
#89075=EDGE_LOOP ( 'NONE', ( #123518, #15395, #11419, #124505 ) ) ;
#89076=VERTEX_POINT ( 'NONE', #94831 ) ;
#89077=AXIS2_PLACEMENT_3D ( 'NONE', #88663, #111837, #44459 ) ;
#89078=CYLINDRICAL_SURFACE ( 'NONE', #124365, 0.5000000000000004441 ) ;
#89079=EDGE_CURVE ( 'NONE', #115930, #103304, #27438, .T. ) ;
#89080=VERTEX_POINT ( 'NONE', #125358 ) ;
#89081=ORIENTED_EDGE ( 'NONE', *, *, #8426, .F. ) ;
#89082=CARTESIAN_POINT ( 'NONE',  ( -35.93988928955958073, -9.740707523384177335, 10.89222023123389427 ) ) ;
#89083=EDGE_LOOP ( 'NONE', ( #2747, #6244, #143210, #21295 ) ) ;
#89084=VECTOR ( 'NONE', #7638, 1000.000000000000227 ) ;
#89086=DIRECTION ( 'NONE',  ( -0.7071067811865487940, 0.7071067811865463515, -0.000000000000000000 ) ) ;
#89087=EDGE_CURVE ( 'NONE', #110076, #121606, #70308, .T. ) ;
#89088=DIRECTION ( 'NONE',  ( -0.7071067811865486830, -0.7071067811865464625, -0.000000000000000000 ) ) ;
#89090=CARTESIAN_POINT ( 'NONE',  ( 34.92499999999998295, -11.14387692260747365, 4.000000000000000000 ) ) ;
#89091=EDGE_LOOP ( 'NONE', ( #47364, #101929, #131856, #78856 ) ) ;
#89092=ORIENTED_EDGE ( 'NONE', *, *, #42105, .F. ) ;
#89094=EDGE_CURVE ( 'NONE', #6909, #69387, #48502, .T. ) ;
#89095=ORIENTED_EDGE ( 'NONE', *, *, #135003, .T. ) ;
#89096=FACE_OUTER_BOUND ( 'NONE', #91868, .T. ) ;
#89098=CARTESIAN_POINT ( 'NONE',  ( 36.48921356237310221, -27.52281430457080802, 5.000000000000000000 ) ) ;
#89099=ORIENTED_EDGE ( 'NONE', *, *, #19685, .T. ) ;
#89100=ORIENTED_EDGE ( 'NONE', *, *, #12093, .F. ) ;
#89103=LINE ( 'NONE', #133324, #106756 ) ;
#89106=DIRECTION ( 'NONE',  ( -0.000000000000000000, 0.3543493200069153248, 0.9351131265310292928 ) ) ;
#89108=CARTESIAN_POINT ( 'NONE',  ( 0.000000000000000000, 0.000000000000000000, 5.000000000000000000 ) ) ;
#89110=CARTESIAN_POINT ( 'NONE',  ( -15.18398860626900237, 28.73617430169797871, 5.000000000000000000 ) ) ;
#89111=DIRECTION ( 'NONE',  ( 0.7071067811865486830, -0.7071067811865464625, -0.000000000000000000 ) ) ;
#89112=LINE ( 'NONE', #10787, #2953 ) ;
#89114=DIRECTION ( 'NONE',  ( 0.7071067811865486830, -0.7071067811865464625, -0.000000000000000000 ) ) ;
#89115=ORIENTED_EDGE ( 'NONE', *, *, #22351, .F. ) ;
#89116=EDGE_CURVE ( 'NONE', #45124, #100098, #108548, .T. ) ;
#89118=CARTESIAN_POINT ( 'NONE',  ( 45.18398860626900415, 28.73617430169818832, 5.000000000000000000 ) ) ;
#89119=ORIENTED_EDGE ( 'NONE', *, *, #56631, .T. ) ;
#89120=ORIENTED_EDGE ( 'NONE', *, *, #92910, .T. ) ;
#89121=VERTEX_POINT ( 'NONE', #118744 ) ;
#89122=DIRECTION ( 'NONE',  ( -0.000000000000000000, -0.3543493200069152693, 0.9351131265310292928 ) ) ;
#89124=VERTEX_POINT ( 'NONE', #96250 ) ;
#89125=DIRECTION ( 'NONE',  ( -0.3543493200069162685, -0.000000000000000000, -0.9351131265310288487 ) ) ;
#89127=DIRECTION ( 'NONE',  ( -0.6830127018922181881, 0.6830127018922202975, -0.2588190451025214056 ) ) ;
#89129=DIRECTION ( 'NONE',  ( -0.7071067811865486830, 0.7071067811865464625, 0.000000000000000000 ) ) ;
#89130=VERTEX_POINT ( 'NONE', #98433 ) ;
#89131=DIRECTION ( 'NONE',  ( -0.7071067811865486830, 0.7071067811865464625, 0.000000000000000000 ) ) ;
#89133=LINE ( 'NONE', #136184, #118623 ) ;
#89135=ORIENTED_EDGE ( 'NONE', *, *, #136972, .F. ) ;
#89138=CARTESIAN_POINT ( 'NONE',  ( -34.45011844616455221, -5.997695858405977631, 5.000000000000000888 ) ) ;
#89139=VERTEX_POINT ( 'NONE', #7832 ) ;
#89140=EDGE_LOOP ( 'NONE', ( #118680, #33123, #128419, #24977 ) ) ;
#89142=CARTESIAN_POINT ( 'NONE',  ( -8.999999999999937828, 8.587461875839158765, 4.000000000000000000 ) ) ;
#89144=CARTESIAN_POINT ( 'NONE',  ( -31.17183060077625711, -11.24070752338416490, 4.000000000000000000 ) ) ;
#89145=DIRECTION ( 'NONE',  ( 0.7071067811865487940, 0.7071067811865463515, 0.000000000000000000 ) ) ;
#89146=EDGE_CURVE ( 'NONE', #52088, #76199, #41923, .T. ) ;
#89147=VERTEX_POINT ( 'NONE', #141965 ) ;
#89148=CARTESIAN_POINT ( 'NONE',  ( -23.99999999999981881, -16.44781430457065952, 5.000000000000000000 ) ) ;
#89149=PLANE ( 'NONE',  #74644 ) ;
#89150=ORIENTED_EDGE ( 'NONE', *, *, #83262, .F. ) ;
#89151=DIRECTION ( 'NONE',  ( 0.7071067811865487940, 0.7071067811865463515, 0.000000000000000000 ) ) ;
#89152=FACE_OUTER_BOUND ( 'NONE', #5678, .T. ) ;
#89153=EDGE_LOOP ( 'NONE', ( #50656, #72748, #56357, #13847 ) ) ;
#89154=PLANE ( 'NONE',  #55640 ) ;
#89155=EDGE_LOOP ( 'NONE', ( #51361, #134707, #134053, #64133, #78083 ) ) ;
#89156=ORIENTED_EDGE ( 'NONE', *, *, #68123, .T. ) ;
#89157=CARTESIAN_POINT ( 'NONE',  ( -6.722814304570563948, -21.72499999999999432, 5.000000000000000000 ) ) ;
#89158=LINE ( 'NONE', #78286, #20554 ) ;
#89159=ORIENTED_EDGE ( 'NONE', *, *, #14908, .F. ) ;
#89160=LINE ( 'NONE', #4944, #44375 ) ;
#89162=CARTESIAN_POINT ( 'NONE',  ( -15.29974487139158867, -27.71228299555216879, 4.000000000000000000 ) ) ;
#89163=AXIS2_PLACEMENT_3D ( 'NONE', #68031, #12856, #55690 ) ;
#89164=EDGE_CURVE ( 'NONE', #63415, #96788, #109304, .T. ) ;
#89165=FACE_OUTER_BOUND ( 'NONE', #97773, .T. ) ;
#89166=FACE_OUTER_BOUND ( 'NONE', #49511, .T. ) ;
#89167=ADVANCED_FACE ( 'NONE', ( #141207 ), #85393, .F. ) ;
#89168=CARTESIAN_POINT ( 'NONE',  ( 16.82816939922341248, 12.75929247661558819, 4.000000000000000000 ) ) ;
#89169=DIRECTION ( 'NONE',  ( -0.000000000000000000, 0.3543493200069153248, 0.9351131265310292928 ) ) ;
#89170=DIRECTION ( 'NONE',  ( 0.6830127018922180770, -0.6830127018922204085, -0.2588190451025213501 ) ) ;
#89172=LINE ( 'NONE', #31227, #92289 ) ;
#89174=LINE ( 'NONE', #86325, #25904 ) ;
#89175=FACE_OUTER_BOUND ( 'NONE', #8700, .T. ) ;
#89176=CARTESIAN_POINT ( 'NONE',  ( -8.241399257801971245, 21.72500000000000142, 5.000000000000000000 ) ) ;
#89178=ADVANCED_FACE ( 'NONE', ( #7094 ), #67996, .T. ) ;
#89179=ORIENTED_EDGE ( 'NONE', *, *, #179, .T. ) ;
#89180=EDGE_CURVE ( 'NONE', #86644, #55203, #33904, .T. ) ;
#89181=ORIENTED_EDGE ( 'NONE', *, *, #19732, .T. ) ;
#89183=ORIENTED_EDGE ( 'NONE', *, *, #1984, .T. ) ;
#89184=VECTOR ( 'NONE', #94308, 1000.000000000000000 ) ;
#89185=EDGE_LOOP ( 'NONE', ( #70750, #2220, #58549, #143068 ) ) ;
#89186=ORIENTED_EDGE ( 'NONE', *, *, #83746, .F. ) ;
#89187=CARTESIAN_POINT ( 'NONE',  ( -17.51078643762690845, -27.52281430457043143, 5.000000000000000000 ) ) ;
#89188=FACE_OUTER_BOUND ( 'NONE', #44216, .T. ) ;
#89189=ORIENTED_EDGE ( 'NONE', *, *, #97849, .T. ) ;
#89190=CARTESIAN_POINT ( 'NONE',  ( -30.88837638105223249, 9.759292476615614831, 17.35367589129219823 ) ) ;
#89191=DIRECTION ( 'NONE',  ( 0.7071067811865487940, -0.7071067811865463515, 0.000000000000000000 ) ) ;
#89192=EDGE_CURVE ( 'NONE', #90802, #61417, #123050, .T. ) ;
#89193=CARTESIAN_POINT ( 'NONE',  ( -0.4892135623730947680, -27.52281430457055578, 5.000000000000000000 ) ) ;
#89194=PLANE ( 'NONE',  #74349 ) ;
#89195=ORIENTED_EDGE ( 'NONE', *, *, #69919, .F. ) ;
#89196=EDGE_CURVE ( 'NONE', #69443, #124524, #2666, .T. ) ;
#89197=CARTESIAN_POINT ( 'NONE',  ( 20.22995720542193254, 21.73644205237998506, 5.000000000000000888 ) ) ;
#89199=DIRECTION ( 'NONE',  ( 0.7071067811865486830, -0.7071067811865464625, -0.000000000000000000 ) ) ;
#89201=DIRECTION ( 'NONE',  ( 0.6830127018922181881, 0.6830127018922202975, -0.2588190451025214056 ) ) ;
#89205=VECTOR ( 'NONE', #56617, 1000.000000000000000 ) ;
#89207=VECTOR ( 'NONE', #6150, 1000.000000000000000 ) ;
#89208=ORIENTED_EDGE ( 'NONE', *, *, #16701, .T. ) ;
#89212=ORIENTED_EDGE ( 'NONE', *, *, #111853, .F. ) ;
#89213=VECTOR ( 'NONE', #58076, 1000.000000000000000 ) ;
#89214=FACE_OUTER_BOUND ( 'NONE', #121874, .T. ) ;
#89215=EDGE_CURVE ( 'NONE', #133767, #23195, #114774, .T. ) ;
#89216=PLANE ( 'NONE',  #17853 ) ;
#89217=DIRECTION ( 'NONE',  ( 0.7071067811865487940, 0.7071067811865463515, -0.000000000000000000 ) ) ;
#89219=ORIENTED_EDGE ( 'NONE', *, *, #1558, .T. ) ;
#89220=ORIENTED_EDGE ( 'NONE', *, *, #78354, .F. ) ;
#89221=EDGE_CURVE ( 'NONE', #46307, #27599, #21592, .T. ) ;
#89223=PLANE ( 'NONE',  #17653 ) ;
#89224=EDGE_LOOP ( 'NONE', ( #119817, #76427, #81838, #12604 ) ) ;
#89225=VERTEX_POINT ( 'NONE', #68682 ) ;
#89229=CARTESIAN_POINT ( 'NONE',  ( -23.99999999999982236, 11.58746187583912324, 4.000000000000000000 ) ) ;
#89230=CARTESIAN_POINT ( 'NONE',  ( 26.99999999999980815, 16.93112307739200872, 4.000000000000000000 ) ) ;
#89234=PLANE ( 'NONE',  #98788 ) ;
#89235=ORIENTED_EDGE ( 'NONE', *, *, #3323, .F. ) ;
#89236=ORIENTED_EDGE ( 'NONE', *, *, #85735, .F. ) ;
#89237=EDGE_LOOP ( 'NONE', ( #138382, #63057, #123626, #102210 ) ) ;
#89238=CARTESIAN_POINT ( 'NONE',  ( -3.489213562373097322, -27.52281430457057709, 5.000000000000000000 ) ) ;
#89239=CARTESIAN_POINT ( 'NONE',  ( -66.18398860626901126, 28.73617430169833753, 5.000000000000000000 ) ) ;
#89240=ORIENTED_EDGE ( 'NONE', *, *, #45338, .F. ) ;
#89241=DIRECTION ( 'NONE',  ( 1.000000000000000000, 0.000000000000000000, 0.000000000000000000 ) ) ;
#89242=EDGE_CURVE ( 'NONE', #15478, #3113, #35349, .T. ) ;
#89243=CARTESIAN_POINT ( 'NONE',  ( -34.92500000000001137, 22.22500000000000142, 4.000000000000000000 ) ) ;
#89245=DIRECTION ( 'NONE',  ( -0.6830127018922180770, -0.6830127018922204085, -0.2588190451025213501 ) ) ;
#89246=FACE_BOUND ( 'NONE', #122087, .T. ) ;
#89247=ORIENTED_EDGE ( 'NONE', *, *, #51762, .F. ) ;
#89250=EDGE_CURVE ( 'NONE', #133772, #30172, #521, .T. ) ;
#89252=PLANE ( 'NONE',  #71712 ) ;
#89253=VERTEX_POINT ( 'NONE', #65852 ) ;
#89254=LINE ( 'NONE', #88560, #15655 ) ;
#89255=ORIENTED_EDGE ( 'NONE', *, *, #121229, .F. ) ;
#89256=ORIENTED_EDGE ( 'NONE', *, *, #3817, .F. ) ;
#89257=VERTEX_POINT ( 'NONE', #1230 ) ;
#89260=EDGE_LOOP ( 'NONE', ( #92878, #38821, #106419, #54871 ) ) ;
#89261=DIRECTION ( 'NONE',  ( 0.7071067811865487940, 0.7071067811865463515, 0.000000000000000000 ) ) ;
#89262=VECTOR ( 'NONE', #20729, 1000.000000000000000 ) ;
#89263=DIRECTION ( 'NONE',  ( -0.7071067811865486830, 0.7071067811865464625, 0.000000000000000000 ) ) ;
#89264=CARTESIAN_POINT ( 'NONE',  ( 57.18398860626899705, 28.73617430169827358, 5.000000000000000000 ) ) ;
#89266=DIRECTION ( 'NONE',  ( -0.6830127018922180770, -0.6830127018922204085, -0.2588190451025213501 ) ) ;
#89267=( BOUNDED_CURVE ( )  B_SPLINE_CURVE ( 3, ( #117689, #130778, #41588, #30745 ),
 .UNSPECIFIED., .F., .T. ) 
 B_SPLINE_CURVE_WITH_KNOTS ( ( 4, 4 ),
 ( 1.901594255663624056, 1.933014472006547635 ),
 .UNSPECIFIED. ) 
 CURVE ( )  GEOMETRIC_REPRESENTATION_ITEM ( )  RATIONAL_B_SPLINE_CURVE ( ( 1.000000000000000000, 0.9999177325257868620, 0.9999177325257868620, 1.000000000000000000 ) ) 
 REPRESENTATION_ITEM ( '' )  );
#89268=DIRECTION ( 'NONE',  ( 1.000000000000000000, 0.000000000000000000, 0.000000000000000000 ) ) ;
#89269=VECTOR ( 'NONE', #89693, 1000.000000000000227 ) ;
#89270=DIRECTION ( 'NONE',  ( -0.6830127018922180770, -0.6830127018922204085, -0.2588190451025213501 ) ) ;
#89271=EDGE_CURVE ( 'NONE', #92661, #98173, #79593, .T. ) ;
#89272=FACE_OUTER_BOUND ( 'NONE', #69629, .T. ) ;
#89273=DIRECTION ( 'NONE',  ( -0.000000000000000000, 1.000000000000000000, -0.000000000000000000 ) ) ;
#89274=ORIENTED_EDGE ( 'NONE', *, *, #28449, .F. ) ;
#89275=EDGE_LOOP ( 'NONE', ( #35806, #60425, #43318, #36887 ) ) ;
#89276=ORIENTED_EDGE ( 'NONE', *, *, #82459, .F. ) ;
#89277=ORIENTED_EDGE ( 'NONE', *, *, #43215, .T. ) ;
#89278=LINE ( 'NONE', #45799, #68202 ) ;
#89279=LINE ( 'NONE', #142941, #123214 ) ;
#89283=EDGE_CURVE ( 'NONE', #97187, #121745, #123776, .T. ) ;
#89284=EDGE_CURVE ( 'NONE', #52318, #106536, #120881, .T. ) ;
#89285=CARTESIAN_POINT ( 'NONE',  ( -5.292893218813417455, 17.25929247661554200, 5.000000000000000000 ) ) ;
#89288=VECTOR ( 'NONE', #98307, 999.9999999999998863 ) ;
#89289=DIRECTION ( 'NONE',  ( -0.000000000000000000, -0.3543493200069152138, 0.9351131265310292928 ) ) ;
#89291=VECTOR ( 'NONE', #86356, 999.9999999999998863 ) ;
#89292=DIRECTION ( 'NONE',  ( -0.7071067811865486830, -0.7071067811865464625, 0.000000000000000000 ) ) ;
#89293=ORIENTED_EDGE ( 'NONE', *, *, #12891, .F. ) ;
#89295=VECTOR ( 'NONE', #49395, 1000.000000000000000 ) ;
#89297=CARTESIAN_POINT ( 'NONE',  ( 34.92499999999998295, 6.006123077391907650, 4.000000000000000000 ) ) ;
#89298=CARTESIAN_POINT ( 'NONE',  ( -34.42500000000001137, -7.458600742197909916, 5.000000000000000000 ) ) ;
#89300=CARTESIAN_POINT ( 'NONE',  ( -17.99999999999987566, 16.55218569542899587, 5.000000000000000000 ) ) ;
#89301=VERTEX_POINT ( 'NONE', #11376 ) ;
#89302=DIRECTION ( 'NONE',  ( -0.7071067811865487940, 0.7071067811865463515, 0.000000000000000000 ) ) ;
#89303=ORIENTED_EDGE ( 'NONE', *, *, #52650, .T. ) ;
#89304=VECTOR ( 'NONE', #49782, 1000.000000000000000 ) ;
#89305=CARTESIAN_POINT ( 'NONE',  ( -24.18398860626899705, 28.73617430169804265, 5.000000000000000000 ) ) ;
#89308=EDGE_CURVE ( 'NONE', #125463, #126916, #46226, .T. ) ;
#89309=ORIENTED_EDGE ( 'NONE', *, *, #35952, .T. ) ;
#89310=LINE ( 'NONE', #58882, #57519 ) ;
#89311=DIRECTION ( 'NONE',  ( -0.000000000000000000, 0.000000000000000000, 1.000000000000000000 ) ) ;
#89312=LINE ( 'NONE', #133537, #2690 ) ;
#89313=ORIENTED_EDGE ( 'NONE', *, *, #47739, .F. ) ;
#89314=CARTESIAN_POINT ( 'NONE',  ( -30.32816939922331301, -6.740707523384216415, 4.000000000000000000 ) ) ;
#89315=EDGE_LOOP ( 'NONE', ( #122948, #136625, #132576, #62727 ) ) ;
#89316=CARTESIAN_POINT ( 'NONE',  ( -36.48921356237310221, -27.52281430457080802, 5.000000000000000000 ) ) ;
#89317=FACE_OUTER_BOUND ( 'NONE', #121418, .T. ) ;
#89318=VERTEX_POINT ( 'NONE', #99112 ) ;
#89321=LINE ( 'NONE', #23327, #32064 ) ;
#89322=VERTEX_POINT ( 'NONE', #12827 ) ;
#89323=LINE ( 'NONE', #49236, #6568 ) ;
#89324=ADVANCED_FACE ( 'NONE', ( #122298 ), #143356, .F. ) ;
#89326=CARTESIAN_POINT ( 'NONE',  ( 60.48921356237309510, -27.52281430457097500, 5.000000000000000000 ) ) ;
#89327=VERTEX_POINT ( 'NONE', #100587 ) ;
#89328=EDGE_CURVE ( 'NONE', #10041, #30236, #45513, .T. ) ;
#89329=CARTESIAN_POINT ( 'NONE',  ( -4.099200028784281358, 22.22500000000000142, 16.68104793800802810 ) ) ;
#89330=CARTESIAN_POINT ( 'NONE',  ( 12.48921356237309155, -27.52281430457064104, 5.000000000000000000 ) ) ;
#89331=CARTESIAN_POINT ( 'NONE',  ( 27.18398860626900060, 28.73617430169806042, 5.000000000000000000 ) ) ;
#89334=LINE ( 'NONE', #99465, #92796 ) ;
#89335=EDGE_CURVE ( 'NONE', #23231, #139660, #3372, .T. ) ;
#89336=EDGE_CURVE ( 'NONE', #48400, #14811, #138204, .T. ) ;
#89337=ORIENTED_EDGE ( 'NONE', *, *, #65602, .T. ) ;
#89338=ORIENTED_EDGE ( 'NONE', *, *, #49382, .T. ) ;
#89340=ORIENTED_EDGE ( 'NONE', *, *, #86582, .F. ) ;
#89341=ORIENTED_EDGE ( 'NONE', *, *, #91168, .F. ) ;
#89343=DIRECTION ( 'NONE',  ( 0.3543493200069162685, -0.000000000000000000, -0.9351131265310288487 ) ) ;
#89344=VERTEX_POINT ( 'NONE', #48337 ) ;
#89345=CARTESIAN_POINT ( 'NONE',  ( -5.510786437626906675, -27.52281430457051314, 5.000000000000000000 ) ) ;
#89347=DIRECTION ( 'NONE',  ( -0.7071067811865486830, -0.7071067811865464625, 0.000000000000000000 ) ) ;
#89348=EDGE_CURVE ( 'NONE', #133793, #116472, #92527, .T. ) ;
#89349=CARTESIAN_POINT ( 'NONE',  ( -31.82816939922330945, 12.75929247661558641, 4.000000000000000000 ) ) ;
#89351=ORIENTED_EDGE ( 'NONE', *, *, #130205, .T. ) ;
#89352=EDGE_CURVE ( 'NONE', #107639, #66777, #47666, .T. ) ;
#89353=DIRECTION ( 'NONE',  ( 0.7071067811865487940, 0.7071067811865463515, 0.000000000000000000 ) ) ;
#89355=CARTESIAN_POINT ( 'NONE',  ( -23.29289321881329045, -3.740707523384244837, 5.000000000000000000 ) ) ;
#89357=LINE ( 'NONE', #108938, #24182 ) ;
#89358=CARTESIAN_POINT ( 'NONE',  ( 5.999999999999958256, 7.552185695429089130, 5.000000000000000000 ) ) ;
#89359=PLANE ( 'NONE',  #43421 ) ;
#89362=CARTESIAN_POINT ( 'NONE',  ( 28.49999999999981171, 3.073033219394654569, -6.593910359670904775 ) ) ;
#89363=DIRECTION ( 'NONE',  ( 0.7071067811865487940, 0.7071067811865463515, 0.000000000000000000 ) ) ;
#89364=ORIENTED_EDGE ( 'NONE', *, *, #70184, .T. ) ;
#89365=VERTEX_POINT ( 'NONE', #25135 ) ;
#89367=EDGE_CURVE ( 'NONE', #104733, #89868, #75035, .T. ) ;
#89368=VECTOR ( 'NONE', #19500, 1000.000000000000227 ) ;
#89369=PLANE ( 'NONE',  #99417 ) ;
#89370=FACE_OUTER_BOUND ( 'NONE', #130193, .T. ) ;
#89371=ORIENTED_EDGE ( 'NONE', *, *, #62878, .T. ) ;
#89372=EDGE_CURVE ( 'NONE', #93963, #70973, #136053, .T. ) ;
#89373=FACE_OUTER_BOUND ( 'NONE', #36422, .T. ) ;
#89375=CARTESIAN_POINT ( 'NONE',  ( -10.49999999999992539, -12.66682484999667579, -0.6294897503864175237 ) ) ;
#89377=VECTOR ( 'NONE', #102561, 1000.000000000000227 ) ;
#89378=ORIENTED_EDGE ( 'NONE', *, *, #126686, .T. ) ;
#89379=EDGE_LOOP ( 'NONE', ( #70441, #36795, #137536, #87107 ) ) ;
#89380=ORIENTED_EDGE ( 'NONE', *, *, #2751, .T. ) ;
#89381=ADVANCED_FACE ( 'NONE', ( #125183 ), #135372, .F. ) ;
#89383=LINE ( 'NONE', #92217, #61594 ) ;
#89384=DIRECTION ( 'NONE',  ( -0.6830127018922180770, 0.6830127018922202975, -0.2588190451025213501 ) ) ;
#89385=ORIENTED_EDGE ( 'NONE', *, *, #91957, .T. ) ;
#89386=LINE ( 'NONE', #57497, #97436 ) ;
#89387=ORIENTED_EDGE ( 'NONE', *, *, #140379, .T. ) ;
#89389=DIRECTION ( 'NONE',  ( -0.6830127018922181881, 0.6830127018922202975, -0.2588190451025214056 ) ) ;
#89390=CARTESIAN_POINT ( 'NONE',  ( -34.47516574401891631, -20.97193265888396496, 4.998110765256836174 ) ) ;
#89391=ADVANCED_FACE ( 'NONE', ( #16388 ), #93970, .F. ) ;
#89392=CARTESIAN_POINT ( 'NONE',  ( 27.18398860626900060, 28.73617430169806042, 5.000000000000000000 ) ) ;
#89393=DIRECTION ( 'NONE',  ( 0.7071067811865487940, -0.7071067811865463515, 0.000000000000000000 ) ) ;
#89394=VECTOR ( 'NONE', #31449, 1000.000000000000000 ) ;
#89395=EDGE_CURVE ( 'NONE', #139596, #137134, #38891, .T. ) ;
#89396=VECTOR ( 'NONE', #113427, 1000.000000000000000 ) ;
#89397=VERTEX_POINT ( 'NONE', #102726 ) ;
#89400=VECTOR ( 'NONE', #97167, 999.9999999999998863 ) ;
#89402=CARTESIAN_POINT ( 'NONE',  ( 13.49999999999991473, -2.947814304570798960, 5.000000000000000000 ) ) ;
#89403=DIRECTION ( 'NONE',  ( -0.000000000000000000, 0.000000000000000000, 1.000000000000000000 ) ) ;
#89404=ORIENTED_EDGE ( 'NONE', *, *, #85374, .F. ) ;
#89406=CYLINDRICAL_SURFACE ( 'NONE', #51653, 0.5000000000000004441 ) ;
#89408=EDGE_CURVE ( 'NONE', #26300, #15282, #70827, .T. ) ;
#89409=EDGE_LOOP ( 'NONE', ( #95684, #47267, #15411, #94594 ) ) ;
#89410=CARTESIAN_POINT ( 'NONE',  ( -14.51078643762690490, -27.52281430457045275, 5.000000000000000000 ) ) ;
#89411=ORIENTED_EDGE ( 'NONE', *, *, #121883, .T. ) ;
#89412=CARTESIAN_POINT ( 'NONE',  ( -2.207106781186520372, -17.24070752338410628, 5.000000000000000000 ) ) ;
#89413=LINE ( 'NONE', #217, #119672 ) ;
#89414=CARTESIAN_POINT ( 'NONE',  ( 33.65494483745361265, 5.259292476615669010, 12.77922209995901603 ) ) ;
#89415=FACE_BOUND ( 'NONE', #55646, .T. ) ;
#89416=PLANE ( 'NONE',  #68900 ) ;
#89418=DIRECTION ( 'NONE',  ( -0.7071067811865486830, -0.7071067811865464625, -0.000000000000000000 ) ) ;
#89419=CARTESIAN_POINT ( 'NONE',  ( -24.29974487139158867, -27.71228299555223273, 4.000000000000000000 ) ) ;
#89421=DIRECTION ( 'NONE',  ( -0.6830127018922180770, -0.6830127018922204085, -0.2588190451025213501 ) ) ;
#89422=ORIENTED_EDGE ( 'NONE', *, *, #69846, .F. ) ;
#89425=ORIENTED_EDGE ( 'NONE', *, *, #27016, .T. ) ;
#89426=FACE_OUTER_BOUND ( 'NONE', #85076, .T. ) ;
#89427=EDGE_CURVE ( 'NONE', #102663, #2265, #137498, .T. ) ;
#89428=ORIENTED_EDGE ( 'NONE', *, *, #107825, .T. ) ;
#89429=FACE_OUTER_BOUND ( 'NONE', #20289, .T. ) ;
#89430=VECTOR ( 'NONE', #104872, 1000.000000000000000 ) ;
#89431=LINE ( 'NONE', #91580, #42652 ) ;
#89432=CARTESIAN_POINT ( 'NONE',  ( 3.618384906019942004, -2.240707523384257716, 13.37739548510238485 ) ) ;
#89433=FACE_OUTER_BOUND ( 'NONE', #84951, .T. ) ;
#89434=DIRECTION ( 'NONE',  ( -0.000000000000000000, 0.000000000000000000, 1.000000000000000000 ) ) ;
#89435=DIRECTION ( 'NONE',  ( -0.6830127018922180770, -0.6830127018922204085, -0.2588190451025213501 ) ) ;
#89436=CARTESIAN_POINT ( 'NONE',  ( -21.79289321881330821, -17.24070752338410628, 5.000000000000000000 ) ) ;
#89439=VECTOR ( 'NONE', #49618, 1000.000000000000000 ) ;
#89440=EDGE_LOOP ( 'NONE', ( #66862, #9907, #26, #82356 ) ) ;
#89441=CARTESIAN_POINT ( 'NONE',  ( 27.29974487139158512, -27.71228299555225405, 4.000000000000000000 ) ) ;
#89442=VERTEX_POINT ( 'NONE', #103403 ) ;
#89443=ORIENTED_EDGE ( 'NONE', *, *, #46847, .F. ) ;
#89444=ORIENTED_EDGE ( 'NONE', *, *, #29895, .F. ) ;
#89445=EDGE_CURVE ( 'NONE', #106219, #21922, #60689, .T. ) ;
#89448=ORIENTED_EDGE ( 'NONE', *, *, #79983, .T. ) ;
#89450=ADVANCED_FACE ( 'NONE', ( #4051 ), #114972, .F. ) ;
#89455=ORIENTED_EDGE ( 'NONE', *, *, #8996, .F. ) ;
#89456=VECTOR ( 'NONE', #143254, 1000.000000000000000 ) ;
#89458=FACE_OUTER_BOUND ( 'NONE', #20624, .T. ) ;
#89459=PLANE ( 'NONE',  #55750 ) ;
#89460=DIRECTION ( 'NONE',  ( -0.7071067811865486830, -0.7071067811865464625, -0.000000000000000000 ) ) ;
#89461=CARTESIAN_POINT ( 'NONE',  ( -29.99451991528749417, 28.92564299267958816, 4.000000000000000000 ) ) ;
#89462=ORIENTED_EDGE ( 'NONE', *, *, #119579, .F. ) ;
#89463=ORIENTED_EDGE ( 'NONE', *, *, #105710, .T. ) ;
#89464=DIRECTION ( 'NONE',  ( 0.7071067811865487940, 0.7071067811865463515, 0.000000000000000000 ) ) ;
#89465=CARTESIAN_POINT ( 'NONE',  ( 0.000000000000000000, 21.72500000000000142, 4.500000000000000888 ) ) ;
#89466=CARTESIAN_POINT ( 'NONE',  ( 0.000000000000000000, 0.000000000000000000, 5.000000000000000000 ) ) ;
#89467=EDGE_CURVE ( 'NONE', #137446, #100841, #124467, .T. ) ;
#89468=ORIENTED_EDGE ( 'NONE', *, *, #140510, .F. ) ;
#89469=CARTESIAN_POINT ( 'NONE',  ( -14.99999999999989342, -18.41253812416056945, 4.000000000000000000 ) ) ;
#89470=DIRECTION ( 'NONE',  ( -0.6830127018922180770, -0.6830127018922204085, -0.2588190451025213501 ) ) ;
#89471=VERTEX_POINT ( 'NONE', #115686 ) ;
#89472=VECTOR ( 'NONE', #56315, 1000.000000000000000 ) ;
#89474=DIRECTION ( 'NONE',  ( -0.7071067811865486830, -0.7071067811865464625, 0.000000000000000000 ) ) ;
#89475=EDGE_CURVE ( 'NONE', #133992, #62201, #5517, .T. ) ;
#89476=CARTESIAN_POINT ( 'NONE',  ( 14.29387692260793763, 22.22500000000000142, 4.000000000000000000 ) ) ;
#89478=CARTESIAN_POINT ( 'NONE',  ( 0.000000000000000000, 0.000000000000000000, 5.000000000000000000 ) ) ;
#89479=CARTESIAN_POINT ( 'NONE',  ( 42.29974487139158157, -27.71228299555235708, 4.000000000000000000 ) ) ;
#89480=AXIS2_PLACEMENT_3D ( 'NONE', #125785, #26460, #138076 ) ;
#89481=LINE ( 'NONE', #17610, #52983 ) ;
#89482=ORIENTED_EDGE ( 'NONE', *, *, #82385, .T. ) ;
#89483=ORIENTED_EDGE ( 'NONE', *, *, #2950, .T. ) ;
#89484=EDGE_CURVE ( 'NONE', #111064, #82851, #113952, .T. ) ;
#89487=AXIS2_PLACEMENT_3D ( 'NONE', #3771, #103809, #46668 ) ;
#89489=PLANE ( 'NONE',  #76059 ) ;
#89493=PLANE ( 'NONE',  #99702 ) ;
#89496=EDGE_CURVE ( 'NONE', #106121, #26065, #138929, .T. ) ;
#89498=CARTESIAN_POINT ( 'NONE',  ( 29.99999999999980105, 2.587461875839216496, 4.000000000000000000 ) ) ;
#89500=LINE ( 'NONE', #122848, #104782 ) ;
#89501=AXIS2_PLACEMENT_3D ( 'NONE', #74568, #107860, #38361 ) ;
#89502=CARTESIAN_POINT ( 'NONE',  ( 18.29974487139159223, -27.71228299555219010, 4.000000000000000000 ) ) ;
#89504=LINE ( 'NONE', #68502, #65002 ) ;
#89505=EDGE_CURVE ( 'NONE', #66379, #142228, #9060, .T. ) ;
#89506=EDGE_CURVE ( 'NONE', #20442, #67467, #52610, .T. ) ;
#89507=LINE ( 'NONE', #88817, #101715 ) ;
#89509=CARTESIAN_POINT ( 'NONE',  ( -23.39513766812465079, 21.75929247661549937, 21.32995629748191746 ) ) ;
#89510=ORIENTED_EDGE ( 'NONE', *, *, #143533, .T. ) ;
#89512=ORIENTED_EDGE ( 'NONE', *, *, #53213, .F. ) ;
#89513=LINE ( 'NONE', #92342, #107925 ) ;
#89514=EDGE_CURVE ( 'NONE', #105535, #14052, #73665, .T. ) ;
#89515=CARTESIAN_POINT ( 'NONE',  ( -11.99999999999991296, -13.97847968911261418, -0.1324546996127068943 ) ) ;
#89516=DIRECTION ( 'NONE',  ( -0.7071067811865486830, 0.7071067811865464625, 0.000000000000000000 ) ) ;
#89518=EDGE_CURVE ( 'NONE', #42670, #90134, #140342, .T. ) ;
#89519=DIRECTION ( 'NONE',  ( 0.7071067811865486830, -0.7071067811865464625, -0.000000000000000000 ) ) ;
#89520=CARTESIAN_POINT ( 'NONE',  ( -5.510786437626906675, -27.52281430457051314, 5.000000000000000000 ) ) ;
#89521=EDGE_LOOP ( 'NONE', ( #125991, #129374, #68469, #75939 ) ) ;
#89522=VERTEX_POINT ( 'NONE', #63535 ) ;
#89523=CARTESIAN_POINT ( 'NONE',  ( -25.49999999999982592, -4.796895815301041033, -3.611700055028741918 ) ) ;
#89527=CARTESIAN_POINT ( 'NONE',  ( -0.7070132642930445632, -21.74070752338405654, 4.999753212805222446 ) ) ;
#89529=CARTESIAN_POINT ( 'NONE',  ( -34.49999999999975842, -10.53574439159939757, 4.994342998332166772 ) ) ;
#89530=DIRECTION ( 'NONE',  ( 1.000000000000000000, 0.000000000000000000, 0.000000000000000000 ) ) ;
#89533=EDGE_CURVE ( 'NONE', #13228, #49400, #62808, .T. ) ;
#89534=CARTESIAN_POINT ( 'NONE',  ( 66.18398860626901126, 28.73617430169833753, 5.000000000000000000 ) ) ;
#89535=DIRECTION ( 'NONE',  ( 0.7071067811865487940, 0.7071067811865463515, 0.000000000000000000 ) ) ;
#89536=CARTESIAN_POINT ( 'NONE',  ( 24.18398860626899705, 28.73617430169804265, 5.000000000000000000 ) ) ;
#89537=ORIENTED_EDGE ( 'NONE', *, *, #18195, .F. ) ;
#89538=EDGE_CURVE ( 'NONE', #88631, #117097, #108381, .T. ) ;
#89539=CARTESIAN_POINT ( 'NONE',  ( -1.171830600776462061, 9.759292476615621936, 4.000000000000000000 ) ) ;
#89540=CARTESIAN_POINT ( 'NONE',  ( -18.00548008471250583, 28.92564299267925776, 4.000000000000000000 ) ) ;
#89542=VECTOR ( 'NONE', #142318, 1000.000000000000000 ) ;
#89543=ORIENTED_EDGE ( 'NONE', *, *, #89467, .F. ) ;
#89544=ORIENTED_EDGE ( 'NONE', *, *, #36190, .F. ) ;
#89545=DIRECTION ( 'NONE',  ( -0.7071067811865486830, -0.7071067811865464625, 0.000000000000000000 ) ) ;
#89548=AXIS2_PLACEMENT_3D ( 'NONE', #110785, #42011, #87638 ) ;
#89549=CARTESIAN_POINT ( 'NONE',  ( -14.99999999999990230, -4.068876922607767455, 4.000000000000000000 ) ) ;
#89550=LINE ( 'NONE', #78683, #58190 ) ;
#89551=DIRECTION ( 'NONE',  ( -0.000000000000000000, 0.3543493200069153248, 0.9351131265310292928 ) ) ;
#89552=ORIENTED_EDGE ( 'NONE', *, *, #71048, .T. ) ;
#89553=CARTESIAN_POINT ( 'NONE',  ( -47.99451991528749062, 28.92564299267971251, 4.000000000000000000 ) ) ;
#89555=LINE ( 'NONE', #114163, #132824 ) ;
#89556=LINE ( 'NONE', #10550, #76233 ) ;
#89557=EDGE_LOOP ( 'NONE', ( #6872, #34287, #76984, #70126 ) ) ;
#89562=ORIENTED_EDGE ( 'NONE', *, *, #80076, .T. ) ;
#89563=VECTOR ( 'NONE', #141670, 1000.000000000000227 ) ;
#89565=FACE_OUTER_BOUND ( 'NONE', #86372, .T. ) ;
#89569=DIRECTION ( 'NONE',  ( 0.7071067811865486830, -0.7071067811865464625, -0.000000000000000000 ) ) ;
#89570=ORIENTED_EDGE ( 'NONE', *, *, #46870, .T. ) ;
#89571=VERTEX_POINT ( 'NONE', #31590 ) ;
#89572=LINE ( 'NONE', #133802, #111674 ) ;
#89573=ORIENTED_EDGE ( 'NONE', *, *, #112693, .T. ) ;
#89574=DIRECTION ( 'NONE',  ( -0.3543493200069162685, -0.000000000000000000, -0.9351131265310288487 ) ) ;
#89575=CARTESIAN_POINT ( 'NONE',  ( -9.707106781186466193, -18.74070752338409207, 5.000000000000000000 ) ) ;
#89576=CARTESIAN_POINT ( 'NONE',  ( 34.92499999999998295, 22.22500000000000142, 4.500000000000000888 ) ) ;
#89577=VERTEX_POINT ( 'NONE', #18526 ) ;
#89578=VECTOR ( 'NONE', #92597, 1000.000000000000000 ) ;
#89579=FACE_BOUND ( 'NONE', #73521, .T. ) ;
#89581=LINE ( 'NONE', #90292, #90611 ) ;
#89582=DIRECTION ( 'NONE',  ( 0.7071067811865487940, 0.7071067811865463515, 0.000000000000000000 ) ) ;
#89584=VECTOR ( 'NONE', #48217, 1000.000000000000227 ) ;
#89585=VECTOR ( 'NONE', #122549, 1000.000000000000000 ) ;
#89588=ORIENTED_EDGE ( 'NONE', *, *, #25642, .T. ) ;
#89592=ORIENTED_EDGE ( 'NONE', *, *, #56191, .T. ) ;
#89593=DIRECTION ( 'NONE',  ( 0.7071067811865487940, 0.7071067811865463515, -0.000000000000000000 ) ) ;
#89594=VERTEX_POINT ( 'NONE', #95402 ) ;
#89595=VECTOR ( 'NONE', #96991, 1000.000000000000227 ) ;
#89597=DIRECTION ( 'NONE',  ( -0.6830127018922181881, 0.6830127018922202975, -0.2588190451025214056 ) ) ;
#89601=EDGE_LOOP ( 'NONE', ( #121129, #95324, #82431, #105170 ) ) ;
#89602=CARTESIAN_POINT ( 'NONE',  ( 34.42499999999998295, -18.02281430457042433, 5.000000000000000000 ) ) ;
#89603=DIRECTION ( 'NONE',  ( 0.7071067811865487940, 0.7071067811865463515, -0.000000000000000000 ) ) ;
#89604=DIRECTION ( 'NONE',  ( -0.000000000000000000, 0.000000000000000000, 1.000000000000000000 ) ) ;
#89606=FACE_OUTER_BOUND ( 'NONE', #36917, .T. ) ;
#89607=CARTESIAN_POINT ( 'NONE',  ( -0.09843580608236146556, 11.25929247661560240, 10.79108189686406938 ) ) ;
#89608=LINE ( 'NONE', #125093, #7396 ) ;
#89609=EDGE_LOOP ( 'NONE', ( #116751, #11645, #56469 ) ) ;
#89611=FACE_OUTER_BOUND ( 'NONE', #95819, .T. ) ;
#89612=EDGE_CURVE ( 'NONE', #874, #31525, #51205, .T. ) ;
#89613=ORIENTED_EDGE ( 'NONE', *, *, #129563, .T. ) ;
#89614=VERTEX_POINT ( 'NONE', #129456 ) ;
#89615=EDGE_CURVE ( 'NONE', #87976, #3063, #119979, .T. ) ;
#89616=ADVANCED_FACE ( 'NONE', ( #30141 ), #41748, .F. ) ;
#89617=EDGE_LOOP ( 'NONE', ( #142546, #7588, #130296, #21296 ) ) ;
#89619=AXIS2_PLACEMENT_3D ( 'NONE', #123363, #68288, #34195 ) ;
#89620=ORIENTED_EDGE ( 'NONE', *, *, #117723, .T. ) ;
#89621=EDGE_CURVE ( 'NONE', #16679, #128612, #109133, .T. ) ;
#89622=EDGE_CURVE ( 'NONE', #61284, #23063, #50487, .T. ) ;
#89623=CARTESIAN_POINT ( 'NONE',  ( -34.49999999999975131, -16.53574439159933718, 4.994342998332169437 ) ) ;
#89627=CARTESIAN_POINT ( 'NONE',  ( 14.99999999999990585, -3.033600742197708477, 5.000000000000000000 ) ) ;
#89628=VERTEX_POINT ( 'NONE', #6923 ) ;
#89629=EDGE_CURVE ( 'NONE', #137290, #131245, #29425, .T. ) ;
#89630=VERTEX_POINT ( 'NONE', #90234 ) ;
#89631=CARTESIAN_POINT ( 'NONE',  ( -2.999999999999975131, 13.93112307739204603, 4.000000000000000000 ) ) ;
#89634=ORIENTED_EDGE ( 'NONE', *, *, #86511, .F. ) ;
#89636=LINE ( 'NONE', #25802, #78459 ) ;
#89637=DIRECTION ( 'NONE',  ( -0.000000000000000000, -0.3543493200069152693, 0.9351131265310292928 ) ) ;
#89638=EDGE_CURVE ( 'NONE', #11133, #3647, #32309, .T. ) ;
#89639=VERTEX_POINT ( 'NONE', #79422 ) ;
#89640=FACE_OUTER_BOUND ( 'NONE', #138367, .T. ) ;
#89641=ORIENTED_EDGE ( 'NONE', *, *, #12976, .T. ) ;
#89643=ORIENTED_EDGE ( 'NONE', *, *, #29268, .F. ) ;
#89644=CARTESIAN_POINT ( 'NONE',  ( -69.29974487139159578, -27.71228299555254537, 4.000000000000000000 ) ) ;
#89645=VECTOR ( 'NONE', #118017, 1000.000000000000227 ) ;
#89646=DIRECTION ( 'NONE',  ( 0.7071067811865487940, 0.7071067811865463515, -0.000000000000000000 ) ) ;
#89648=LINE ( 'NONE', #57060, #4641 ) ;
#89649=CARTESIAN_POINT ( 'NONE',  ( -45.18398860626900415, 28.73617430169818832, 5.000000000000000000 ) ) ;
#89650=EDGE_LOOP ( 'NONE', ( #85118, #100704, #95207, #6050 ) ) ;
#89652=CARTESIAN_POINT ( 'NONE',  ( 10.36246187583895306, 22.22500000000000142, 4.000000000000000000 ) ) ;
#89655=CARTESIAN_POINT ( 'NONE',  ( -23.36654548503486950, 7.297668562427137573, 4.000000000000000000 ) ) ;
#89658=VERTEX_POINT ( 'NONE', #46054 ) ;
#89659=ORIENTED_EDGE ( 'NONE', *, *, #14030, .F. ) ;
#89660=EDGE_CURVE ( 'NONE', #26438, #52182, #123619, .T. ) ;
#89661=VERTEX_POINT ( 'NONE', #99675 ) ;
#89663=DIRECTION ( 'NONE',  ( -0.7071067811865486830, 0.7071067811865464625, 0.000000000000000000 ) ) ;
#89665=DIRECTION ( 'NONE',  ( -0.7071067811865486830, -0.7071067811865464625, 0.000000000000000000 ) ) ;
#89666=LINE ( 'NONE', #132507, #50571 ) ;
#89668=EDGE_CURVE ( 'NONE', #117033, #45436, #55492, .T. ) ;
#89669=CARTESIAN_POINT ( 'NONE',  ( 9.328169399223467551, 8.259292476615627265, 4.000000000000000000 ) ) ;
#89670=CARTESIAN_POINT ( 'NONE',  ( 2.671830600776447628, -18.74070752338408852, 4.000000000000000000 ) ) ;
#89671=DIRECTION ( 'NONE',  ( -0.7071067811865486830, 0.7071067811865464625, 0.000000000000000000 ) ) ;
#89674=VERTEX_POINT ( 'NONE', #43897 ) ;
#89675=FACE_OUTER_BOUND ( 'NONE', #67557, .T. ) ;
#89676=ORIENTED_EDGE ( 'NONE', *, *, #110091, .T. ) ;
#89679=EDGE_CURVE ( 'NONE', #86675, #75683, #11951, .T. ) ;
#89680=DIRECTION ( 'NONE',  ( -0.000000000000000000, -0.000000000000000000, 1.000000000000000000 ) ) ;
#89681=FACE_OUTER_BOUND ( 'NONE', #33629, .T. ) ;
#89682=VERTEX_POINT ( 'NONE', #131619 ) ;
#89684=LINE ( 'NONE', #123768, #101960 ) ;
#89686=ORIENTED_EDGE ( 'NONE', *, *, #57901, .F. ) ;
#89689=VERTEX_POINT ( 'NONE', #1754 ) ;
#89690=ADVANCED_FACE ( 'NONE', ( #98276 ), #45349, .F. ) ;
#89691=VECTOR ( 'NONE', #104387, 999.9999999999998863 ) ;
#89692=AXIS2_PLACEMENT_3D ( 'NONE', #84095, #117370, #18044 ) ;
#89693=DIRECTION ( 'NONE',  ( -0.3543493200069163240, -0.000000000000000000, -0.9351131265310288487 ) ) ;
#89696=VERTEX_POINT ( 'NONE', #121434 ) ;
#89697=EDGE_CURVE ( 'NONE', #3281, #51730, #33748, .T. ) ;
#89699=PLANE ( 'NONE',  #31121 ) ;
#89700=PLANE ( 'NONE',  #57774 ) ;
#89705=CARTESIAN_POINT ( 'NONE',  ( 2.999999999999981792, -10.44781430457072169, 5.000000000000000000 ) ) ;
#89706=ORIENTED_EDGE ( 'NONE', *, *, #15205, .T. ) ;
#89707=ORIENTED_EDGE ( 'NONE', *, *, #15855, .F. ) ;
#89708=CARTESIAN_POINT ( 'NONE',  ( 1.889826771117872006, -22.22500000000000497, 4.785647885939354751 ) ) ;
#89709=EDGE_LOOP ( 'NONE', ( #69278, #27539, #139635, #78940 ) ) ;
#89711=CARTESIAN_POINT ( 'NONE',  ( -45.18398860626900415, 28.73617430169818832, 5.000000000000000000 ) ) ;
#89712=CARTESIAN_POINT ( 'NONE',  ( -14.99451991528749595, 28.92564299267948513, 4.000000000000000000 ) ) ;
#89715=VERTEX_POINT ( 'NONE', #76538 ) ;
#89718=CARTESIAN_POINT ( 'NONE',  ( -27.48921356237309155, -27.52281430457074762, 5.000000000000000000 ) ) ;
#89719=EDGE_CURVE ( 'NONE', #53420, #40404, #34437, .T. ) ;
#89720=DIRECTION ( 'NONE',  ( 0.6830127018922181881, 0.6830127018922202975, -0.2588190451025214056 ) ) ;
#89721=CARTESIAN_POINT ( 'NONE',  ( -16.49999999999987210, -17.94781430457065241, 5.000000000000000000 ) ) ;
#89722=DIRECTION ( 'NONE',  ( 0.000000000000000000, 1.000000000000000000, 0.000000000000000000 ) ) ;
#89723=ORIENTED_EDGE ( 'NONE', *, *, #92394, .T. ) ;
#89725=VECTOR ( 'NONE', #38104, 999.9999999999998863 ) ;
#89726=CARTESIAN_POINT ( 'NONE',  ( 34.92499999999998295, -1.298069433179003695, 4.500000000000000888 ) ) ;
#89727=CARTESIAN_POINT ( 'NONE',  ( -12.48921356237309155, -27.52281430457064104, 5.000000000000000000 ) ) ;
#89728=DIRECTION ( 'NONE',  ( 0.6830127018922180770, -0.6830127018922204085, -0.2588190451025213501 ) ) ;
#89729=CARTESIAN_POINT ( 'NONE',  ( 26.99999999999981526, -21.41253812416053748, 4.000000000000000000 ) ) ;
#89731=ADVANCED_FACE ( 'NONE', ( #120713 ), #122869, .T. ) ;
#89733=EDGE_LOOP ( 'NONE', ( #17752, #29476, #108162, #63963 ) ) ;
#89735=VECTOR ( 'NONE', #143508, 999.9999999999998863 ) ;
#89736=ORIENTED_EDGE ( 'NONE', *, *, #113061, .T. ) ;
#89737=LINE ( 'NONE', #123820, #69460 ) ;
#89738=DIRECTION ( 'NONE',  ( 0.7071067811865486830, -0.7071067811865464625, -0.000000000000000000 ) ) ;
#89739=LINE ( 'NONE', #133961, #59631 ) ;
#89740=CARTESIAN_POINT ( 'NONE',  ( 51.48921356237309510, -27.52281430457091460, 5.000000000000000000 ) ) ;
#89741=ORIENTED_EDGE ( 'NONE', *, *, #97132, .T. ) ;
#89743=DIRECTION ( 'NONE',  ( -0.3543493200069162685, -0.000000000000000000, -0.9351131265310288487 ) ) ;
#89746=EDGE_CURVE ( 'NONE', #46825, #14025, #67823, .T. ) ;
#89747=VERTEX_POINT ( 'NONE', #77952 ) ;
#89748=LINE ( 'NONE', #42706, #129962 ) ;
#89749=CARTESIAN_POINT ( 'NONE',  ( -11.81601139373100651, 28.73617430169779041, 5.000000000000000000 ) ) ;
#89750=ORIENTED_EDGE ( 'NONE', *, *, #123938, .F. ) ;
#89751=EDGE_LOOP ( 'NONE', ( #95885, #57758, #124698, #7017 ) ) ;
#89752=DIRECTION ( 'NONE',  ( 0.7071067811865487940, 0.7071067811865463515, 0.000000000000000000 ) ) ;
#89753=EDGE_CURVE ( 'NONE', #83353, #106932, #9819, .T. ) ;
#89754=DIRECTION ( 'NONE',  ( 0.6830127018922180770, -0.6830127018922204085, -0.2588190451025213501 ) ) ;
#89755=CARTESIAN_POINT ( 'NONE',  ( -9.156123077392344101, -22.22500000000000142, 4.000000000000000000 ) ) ;
#89757=LINE ( 'NONE', #101350, #109889 ) ;
#89758=ORIENTED_EDGE ( 'NONE', *, *, #69315, .T. ) ;
#89759=ORIENTED_EDGE ( 'NONE', *, *, #12893, .F. ) ;
#89760=CARTESIAN_POINT ( 'NONE',  ( 12.70710678118645909, -6.740707523384214639, 5.000000000000000000 ) ) ;
#89761=ORIENTED_EDGE ( 'NONE', *, *, #112910, .F. ) ;
#89763=FACE_OUTER_BOUND ( 'NONE', #63973, .T. ) ;
#89764=ORIENTED_EDGE ( 'NONE', *, *, #51908, .T. ) ;
#89765=CARTESIAN_POINT ( 'NONE',  ( 8.700255128608413102, -27.71228299555199825, 4.000000000000000000 ) ) ;
#89766=DIRECTION ( 'NONE',  ( 0.7071067811865487940, 0.7071067811865463515, 0.000000000000000000 ) ) ;
#89767=DIRECTION ( 'NONE',  ( 0.3543493200069162685, -0.000000000000000000, -0.9351131265310288487 ) ) ;
#89768=CARTESIAN_POINT ( 'NONE',  ( 24.87009481391959298, 1.845822036158552892, 4.338987337627242091 ) ) ;
#89769=EDGE_CURVE ( 'NONE', #89870, #81077, #132360, .T. ) ;
#89770=VECTOR ( 'NONE', #67185, 1000.000000000000000 ) ;
#89772=ORIENTED_EDGE ( 'NONE', *, *, #141435, .F. ) ;
#89774=ORIENTED_EDGE ( 'NONE', *, *, #107961, .F. ) ;
#89775=DIRECTION ( 'NONE',  ( -0.7071067811865486830, -0.7071067811865464625, 0.000000000000000000 ) ) ;
#89776=ORIENTED_EDGE ( 'NONE', *, *, #118180, .T. ) ;
#89777=PLANE ( 'NONE',  #2825 ) ;
#89779=ORIENTED_EDGE ( 'NONE', *, *, #95939, .T. ) ;
#89780=DIRECTION ( 'NONE',  ( -0.000000000000000000, -0.3543493200069152693, 0.9351131265310292928 ) ) ;
#89781=VERTEX_POINT ( 'NONE', #22801 ) ;
#89782=ORIENTED_EDGE ( 'NONE', *, *, #106642, .T. ) ;
#89783=VECTOR ( 'NONE', #78574, 1000.000000000000000 ) ;
#89784=VERTEX_POINT ( 'NONE', #10517 ) ;
#89785=VECTOR ( 'NONE', #96519, 1000.000000000000114 ) ;
#89786=EDGE_CURVE ( 'NONE', #123983, #117224, #95979, .T. ) ;
#89787=ADVANCED_FACE ( 'NONE', ( #137330 ), #69967, .F. ) ;
#89788=PLANE ( 'NONE',  #62826 ) ;
#89789=LINE ( 'NONE', #23076, #36735 ) ;
#89790=DIRECTION ( 'NONE',  ( -0.7071067811865486830, -0.7071067811865464625, 0.000000000000000000 ) ) ;
#89793=CARTESIAN_POINT ( 'NONE',  ( -42.48921356237308800, -27.52281430457085065, 5.000000000000000000 ) ) ;
#89794=EDGE_CURVE ( 'NONE', #95118, #55534, #127139, .T. ) ;
#89795=DIRECTION ( 'NONE',  ( 0.7071067811865487940, -0.7071067811865463515, 0.000000000000000000 ) ) ;
#89796=EDGE_CURVE ( 'NONE', #47233, #1370, #115515, .T. ) ;
#89797=LINE ( 'NONE', #32589, #60971 ) ;
#89798=CARTESIAN_POINT ( 'NONE',  ( -56.99451991528749062, 28.92564299267978001, 4.000000000000000000 ) ) ;
#89799=EDGE_CURVE ( 'NONE', #41140, #85990, #27835, .T. ) ;
#89800=VERTEX_POINT ( 'NONE', #112704 ) ;
#89801=CARTESIAN_POINT ( 'NONE',  ( -27.48921356237309155, -27.52281430457074762, 5.000000000000000000 ) ) ;
#89802=FACE_OUTER_BOUND ( 'NONE', #5832, .T. ) ;
#89803=CARTESIAN_POINT ( 'NONE',  ( -36.18398860626899705, 28.73617430169812437, 5.000000000000000000 ) ) ;
#89804=VERTEX_POINT ( 'NONE', #103244 ) ;
#89805=VERTEX_POINT ( 'NONE', #3893 ) ;
#89806=DIRECTION ( 'NONE',  ( 0.7071067811865487940, 0.7071067811865463515, 0.000000000000000000 ) ) ;
#89807=ORIENTED_EDGE ( 'NONE', *, *, #54693, .T. ) ;
#89808=ORIENTED_EDGE ( 'NONE', *, *, #125748, .T. ) ;
#89809=FACE_OUTER_BOUND ( 'NONE', #129661, .T. ) ;
#89811=EDGE_CURVE ( 'NONE', #5696, #114242, #46799, .T. ) ;
#89812=LINE ( 'NONE', #134056, #65787 ) ;
#89813=DIRECTION ( 'NONE',  ( -0.7071067811865487940, 0.7071067811865463515, 0.000000000000000000 ) ) ;
#89814=VERTEX_POINT ( 'NONE', #4587 ) ;
#89816=DIRECTION ( 'NONE',  ( 0.7071067811865487940, 0.7071067811865463515, 0.000000000000000000 ) ) ;
#89817=ORIENTED_EDGE ( 'NONE', *, *, #107627, .T. ) ;
#89818=ADVANCED_FACE ( 'NONE', ( #125744 ), #38024, .T. ) ;
#89819=LINE ( 'NONE', #102861, #44581 ) ;
#89821=ORIENTED_EDGE ( 'NONE', *, *, #80129, .F. ) ;
#89823=DIRECTION ( 'NONE',  ( -0.7071067811865486830, -0.7071067811865463515, 0.000000000000000000 ) ) ;
#89824=FACE_OUTER_BOUND ( 'NONE', #120252, .T. ) ;
#89825=ORIENTED_EDGE ( 'NONE', *, *, #82185, .F. ) ;
#89826=ORIENTED_EDGE ( 'NONE', *, *, #70549, .T. ) ;
#89827=ORIENTED_EDGE ( 'NONE', *, *, #62059, .T. ) ;
#89828=DIRECTION ( 'NONE',  ( -0.6830127018922180770, -0.6830127018922204085, -0.2588190451025213501 ) ) ;
#89830=LINE ( 'NONE', #65266, #82101 ) ;
#89831=LINE ( 'NONE', #123212, #63550 ) ;
#89832=VERTEX_POINT ( 'NONE', #92358 ) ;
#89833=AXIS2_PLACEMENT_3D ( 'NONE', #34412, #110514, #133042 ) ;
#89834=CARTESIAN_POINT ( 'NONE',  ( -13.11345250541376473, 3.796869306786347487, 4.054893674211258237 ) ) ;
#89835=CARTESIAN_POINT ( 'NONE',  ( -36.48921356237310221, -27.52281430457080802, 5.000000000000000000 ) ) ;
#89836=CARTESIAN_POINT ( 'NONE',  ( 23.29298673570678346, -21.74070752338406720, 4.999753212805222446 ) ) ;
#89837=ADVANCED_FACE ( 'NONE', ( #136586 ), #81541, .F. ) ;
#89838=VERTEX_POINT ( 'NONE', #104678 ) ;
#89839=PLANE ( 'NONE',  #109073 ) ;
#89841=ORIENTED_EDGE ( 'NONE', *, *, #62687, .F. ) ;
#89842=ADVANCED_FACE ( 'NONE', ( #114811 ), #5346, .F. ) ;
#89843=DIRECTION ( 'NONE',  ( -0.7071067811865487940, 0.7071067811865463515, 0.000000000000000000 ) ) ;
#89844=EDGE_LOOP ( 'NONE', ( #11301, #60683, #59075, #78455 ) ) ;
#89845=VERTEX_POINT ( 'NONE', #113406 ) ;
#89846=DIRECTION ( 'NONE',  ( 0.3543493200069162685, -0.000000000000000000, -0.9351131265310288487 ) ) ;
#89847=PLANE ( 'NONE',  #29868 ) ;
#89848=ORIENTED_EDGE ( 'NONE', *, *, #6680, .T. ) ;
#89851=EDGE_CURVE ( 'NONE', #89661, #84730, #47504, .T. ) ;
#89852=DIRECTION ( 'NONE',  ( 0.6830127018922180770, -0.6830127018922204085, -0.2588190451025213501 ) ) ;
#89853=CARTESIAN_POINT ( 'NONE',  ( -29.67183060077625711, 20.25929247661551003, 4.000000000000000000 ) ) ;
#89854=DIRECTION ( 'NONE',  ( 0.7071067811865487940, 0.7071067811865463515, 0.000000000000000000 ) ) ;
#89855=VECTOR ( 'NONE', #20595, 1000.000000000000000 ) ;
#89857=DIRECTION ( 'NONE',  ( 0.7071067811865487940, -0.7071067811865463515, 0.000000000000000000 ) ) ;
#89858=ADVANCED_FACE ( 'NONE', ( #48894 ), #49631, .F. ) ;
#89859=FACE_OUTER_BOUND ( 'NONE', #78246, .T. ) ;
#89860=DIRECTION ( 'NONE',  ( 0.7071067811865486830, -0.7071067811865464625, -0.000000000000000000 ) ) ;
#89864=DIRECTION ( 'NONE',  ( 0.6830127018922181881, 0.6830127018922202975, -0.2588190451025214056 ) ) ;
#89866=DIRECTION ( 'NONE',  ( -0.6830127018922180770, -0.6830127018922204085, -0.2588190451025213501 ) ) ;
#89867=ORIENTED_EDGE ( 'NONE', *, *, #88926, .F. ) ;
#89868=VERTEX_POINT ( 'NONE', #36567 ) ;
#89870=VERTEX_POINT ( 'NONE', #135208 ) ;
#89871=ORIENTED_EDGE ( 'NONE', *, *, #134555, .T. ) ;
#89872=EDGE_CURVE ( 'NONE', #36166, #15951, #138034, .T. ) ;
#89873=VERTEX_POINT ( 'NONE', #80814 ) ;
#89874=CARTESIAN_POINT ( 'NONE',  ( 12.18398860626900060, 28.73617430169795739, 5.000000000000000000 ) ) ;
#89875=CARTESIAN_POINT ( 'NONE',  ( 17.30673006690389926, -3.740707523384244837, 12.88036043432863664 ) ) ;
#89876=CARTESIAN_POINT ( 'NONE',  ( -18.72281430457046270, -21.72500000000000142, 5.000000000000000000 ) ) ;
#89877=VERTEX_POINT ( 'NONE', #80113 ) ;
#89878=AXIS2_PLACEMENT_3D ( 'NONE', #7056, #85361, #140463 ) ;
#89879=LINE ( 'NONE', #134863, #76489 ) ;
#89880=CARTESIAN_POINT ( 'NONE',  ( -6.524001385854439228, 22.03583458319438293, 4.979811245910091166 ) ) ;
#89881=VECTOR ( 'NONE', #36626, 1000.000000000000000 ) ;
#89882=DIRECTION ( 'NONE',  ( 0.7071067811865486830, -0.7071067811865464625, -0.000000000000000000 ) ) ;
#89883=DIRECTION ( 'NONE',  ( -0.000000000000000000, -0.3543493200069152693, 0.9351131265310292928 ) ) ;
#89885=ORIENTED_EDGE ( 'NONE', *, *, #16717, .T. ) ;
#89886=EDGE_CURVE ( 'NONE', #31340, #8931, #124296, .T. ) ;
#89887=PLANE ( 'NONE',  #78864 ) ;
#89888=LINE ( 'NONE', #97354, #72491 ) ;
#89889=PLANE ( 'NONE',  #130678 ) ;
#89890=AXIS2_PLACEMENT_3D ( 'NONE', #71618, #16483, #60779 ) ;
#89892=LINE ( 'NONE', #36940, #12219 ) ;
#89893=CARTESIAN_POINT ( 'NONE',  ( 29.18753812416031934, -22.22500000000000497, 4.000000000000000000 ) ) ;
#89894=VECTOR ( 'NONE', #129715, 1000.000000000000000 ) ;
#89895=FACE_OUTER_BOUND ( 'NONE', #111730, .T. ) ;
#89896=CARTESIAN_POINT ( 'NONE',  ( 8.994519915287490619, 28.92564299267944250, 4.000000000000000000 ) ) ;
#89897=ADVANCED_FACE ( 'NONE', ( #106805 ), #84391, .F. ) ;
#89898=ORIENTED_EDGE ( 'NONE', *, *, #143283, .F. ) ;
#89899=ORIENTED_EDGE ( 'NONE', *, *, #82063, .F. ) ;
#89901=ORIENTED_EDGE ( 'NONE', *, *, #101575, .F. ) ;
#89903=AXIS2_PLACEMENT_3D ( 'NONE', #61203, #28535, #93062 ) ;
#89905=CARTESIAN_POINT ( 'NONE',  ( 60.29974487139158867, -27.71228299555248142, 4.000000000000000000 ) ) ;
#89906=CARTESIAN_POINT ( 'NONE',  ( -13.49999999999990763, 13.46639925780212366, 5.000000000000000000 ) ) ;
#89907=EDGE_CURVE ( 'NONE', #116519, #29125, #19099, .T. ) ;
#89908=VECTOR ( 'NONE', #130367, 999.9999999999998863 ) ;
#89910=EDGE_CURVE ( 'NONE', #86031, #60612, #42310, .T. ) ;
#89911=EDGE_LOOP ( 'NONE', ( #13655, #40954, #90126 ) ) ;
#89912=EDGE_LOOP ( 'NONE', ( #121679, #127910, #133856, #68786 ) ) ;
#89913=CARTESIAN_POINT ( 'NONE',  ( -30.48921356237309510, -27.52281430457076894, 5.000000000000000000 ) ) ;
#89916=VERTEX_POINT ( 'NONE', #29256 ) ;
#89918=ORIENTED_EDGE ( 'NONE', *, *, #94572, .T. ) ;
#89919=DIRECTION ( 'NONE',  ( 0.000000000000000000, 0.000000000000000000, 1.000000000000000000 ) ) ;
#89920=EDGE_CURVE ( 'NONE', #51650, #138101, #74207, .T. ) ;
#89923=ORIENTED_EDGE ( 'NONE', *, *, #3985, .T. ) ;
#89926=VERTEX_POINT ( 'NONE', #41556 ) ;
#89927=VECTOR ( 'NONE', #10784, 1000.000000000000000 ) ;
#89928=ORIENTED_EDGE ( 'NONE', *, *, #75387, .F. ) ;
#89929=VECTOR ( 'NONE', #77758, 999.9999999999998863 ) ;
#89931=CARTESIAN_POINT ( 'NONE',  ( -30.48921356237309510, -27.52281430457076894, 5.000000000000000000 ) ) ;
#89932=ORIENTED_EDGE ( 'NONE', *, *, #96324, .F. ) ;
#89933=CARTESIAN_POINT ( 'NONE',  ( 17.64297733114876365, -22.22500000000000142, -14.91997170495656277 ) ) ;
#89935=DIRECTION ( 'NONE',  ( 0.6830127018922181881, 0.6830127018922202975, -0.2588190451025214056 ) ) ;
#89936=CARTESIAN_POINT ( 'NONE',  ( -0.7071067811865372477, -12.74070752338415424, 5.000000000000000000 ) ) ;
#89937=FACE_BOUND ( 'NONE', #41268, .T. ) ;
#89938=EDGE_LOOP ( 'NONE', ( #54305, #15204, #133348, #78198 ) ) ;
#89939=CARTESIAN_POINT ( 'NONE',  ( -12.32816939922344268, -6.740707523384212863, 4.000000000000000000 ) ) ;
#89940=CARTESIAN_POINT ( 'NONE',  ( 57.18398860626899705, 28.73617430169827358, 5.000000000000000000 ) ) ;
#89941=CARTESIAN_POINT ( 'NONE',  ( 27.48921356237309155, -27.52281430457074762, 5.000000000000000000 ) ) ;
#89942=ORIENTED_EDGE ( 'NONE', *, *, #74001, .F. ) ;
#89943=DIRECTION ( 'NONE',  ( 0.6830127018922181881, 0.6830127018922202975, -0.2588190451025214056 ) ) ;
#89944=ORIENTED_EDGE ( 'NONE', *, *, #106316, .T. ) ;
#89945=EDGE_LOOP ( 'NONE', ( #21933, #17788, #138413, #120644 ) ) ;
#89946=VERTEX_POINT ( 'NONE', #86520 ) ;
#89947=EDGE_CURVE ( 'NONE', #97043, #61191, #73499, .T. ) ;
#89949=VERTEX_POINT ( 'NONE', #119122 ) ;
#89950=PLANE ( 'NONE',  #106530 ) ;
#89951=EDGE_CURVE ( 'NONE', #32782, #17436, #128770, .T. ) ;
#89952=ADVANCED_FACE ( 'NONE', ( #117663 ), #94504, .F. ) ;
#89953=DIRECTION ( 'NONE',  ( -0.7071067811865487940, 0.7071067811865463515, 0.000000000000000000 ) ) ;
#89954=ORIENTED_EDGE ( 'NONE', *, *, #140727, .T. ) ;
#89955=EDGE_CURVE ( 'NONE', #49015, #1952, #130746, .T. ) ;
#89957=DIRECTION ( 'NONE',  ( 0.3543493200069162685, -0.000000000000000000, -0.9351131265310288487 ) ) ;
#89959=DIRECTION ( 'NONE',  ( -0.7071067811865486830, -0.7071067811865464625, 0.000000000000000000 ) ) ;
#89964=VERTEX_POINT ( 'NONE', #7494 ) ;
#89965=ORIENTED_EDGE ( 'NONE', *, *, #13916, .T. ) ;
#89966=EDGE_LOOP ( 'NONE', ( #3988, #129160, #36235, #131424 ) ) ;
#89967=CARTESIAN_POINT ( 'NONE',  ( -66.29974487139159578, -27.71228299555252406, 4.000000000000000000 ) ) ;
#89968=VECTOR ( 'NONE', #36816, 1000.000000000000000 ) ;
#89969=VECTOR ( 'NONE', #42621, 1000.000000000000000 ) ;
#89970=ORIENTED_EDGE ( 'NONE', *, *, #21019, .T. ) ;
#89971=VECTOR ( 'NONE', #128990, 1000.000000000000000 ) ;
#89972=AXIS2_PLACEMENT_3D ( 'NONE', #22167, #43956, #52670 ) ;
#89973=EDGE_LOOP ( 'NONE', ( #106093, #134855, #59841, #51229 ) ) ;
#89975=ADVANCED_FACE ( 'NONE', ( #19803 ), #108211, .F. ) ;
#89976=ADVANCED_FACE ( 'NONE', ( #107532 ), #140179, .F. ) ;
#89977=FACE_OUTER_BOUND ( 'NONE', #114747, .T. ) ;
#89978=VERTEX_POINT ( 'NONE', #129275 ) ;
#89979=CARTESIAN_POINT ( 'NONE',  ( -9.656710001662071718, 3.759292476615678336, 13.27625715073263457 ) ) ;
#89980=AXIS2_PLACEMENT_3D ( 'NONE', #82685, #49369, #40611 ) ;
#89981=VECTOR ( 'NONE', #26396, 1000.000000000000000 ) ;
#89982=EDGE_CURVE ( 'NONE', #31545, #36043, #85779, .T. ) ;
#89983=CARTESIAN_POINT ( 'NONE',  ( -0.1839886062690032631, 28.73617430169787568, 5.000000000000000000 ) ) ;
#89985=DIRECTION ( 'NONE',  ( -0.6830127018922181881, 0.6830127018922202975, -0.2588190451025214056 ) ) ;
#89986=VERTEX_POINT ( 'NONE', #64044 ) ;
#89988=CARTESIAN_POINT ( 'NONE',  ( 19.05000000000000071, 3.174999999999997158, 5.000000000000000000 ) ) ;
#89989=LINE ( 'NONE', #113898, #23302 ) ;
#89991=ADVANCED_FACE ( 'NONE', ( #28569 ), #72828, .F. ) ;
#89992=DIRECTION ( 'NONE',  ( 0.7071067811865487940, 0.7071067811865463515, -0.000000000000000000 ) ) ;
#89993=ORIENTED_EDGE ( 'NONE', *, *, #98511, .T. ) ;
#89997=ORIENTED_EDGE ( 'NONE', *, *, #101087, .T. ) ;
#89998=LINE ( 'NONE', #100190, #77526 ) ;
#89999=DIRECTION ( 'NONE',  ( 0.7071067811865487940, -0.7071067811865463515, 0.000000000000000000 ) ) ;
#90000=LINE ( 'NONE', #13141, #118973 ) ;
#90001=ORIENTED_EDGE ( 'NONE', *, *, #33554, .T. ) ;
#90002=CARTESIAN_POINT ( 'NONE',  ( -17.29289321881332953, -3.740707523384248390, 5.000000000000000000 ) ) ;
#90003=CARTESIAN_POINT ( 'NONE',  ( -53.99451991528749062, 28.92564299267975869, 4.000000000000000000 ) ) ;
#90004=DIRECTION ( 'NONE',  ( -0.7071067811865486830, 0.7071067811865464625, 0.000000000000000000 ) ) ;
#90005=EDGE_CURVE ( 'NONE', #133772, #63910, #77086, .T. ) ;
#90006=VERTEX_POINT ( 'NONE', #31416 ) ;
#90007=VECTOR ( 'NONE', #16014, 1000.000000000000227 ) ;
#90008=AXIS2_PLACEMENT_3D ( 'NONE', #69801, #70529, #115360 ) ;
#90009=LINE ( 'NONE', #24763, #132638 ) ;
#90010=VECTOR ( 'NONE', #109293, 999.9999999999998863 ) ;
#90011=ORIENTED_EDGE ( 'NONE', *, *, #34479, .F. ) ;
#90012=VECTOR ( 'NONE', #6191, 1000.000000000000000 ) ;
#90014=PLANE ( 'NONE',  #25499 ) ;
#90016=ORIENTED_EDGE ( 'NONE', *, *, #116405, .F. ) ;
#90017=LINE ( 'NONE', #134263, #65838 ) ;
#90019=LINE ( 'NONE', #135000, #34343 ) ;
#90020=ORIENTED_EDGE ( 'NONE', *, *, #100296, .T. ) ;
#90021=VECTOR ( 'NONE', #81990, 1000.000000000000227 ) ;
#90022=DIRECTION ( 'NONE',  ( 0.7071067811865487940, 0.7071067811865463515, 0.000000000000000000 ) ) ;
#90024=DIRECTION ( 'NONE',  ( -0.7071067811865486830, -0.7071067811865464625, -0.000000000000000000 ) ) ;
#90025=ORIENTED_EDGE ( 'NONE', *, *, #56926, .F. ) ;
#90026=CARTESIAN_POINT ( 'NONE',  ( 60.29974487139158867, -27.71228299555248142, 4.000000000000000000 ) ) ;
#90027=ADVANCED_FACE ( 'NONE', ( #67644 ), #76349, .F. ) ;
#90028=PLANE ( 'NONE',  #32837 ) ;
#90029=DIRECTION ( 'NONE',  ( -0.7071067811865486830, -0.7071067811865464625, 0.000000000000000000 ) ) ;
#90030=VECTOR ( 'NONE', #101060, 1000.000000000000000 ) ;
#90032=FACE_OUTER_BOUND ( 'NONE', #13218, .T. ) ;
#90035=ORIENTED_EDGE ( 'NONE', *, *, #37186, .F. ) ;
#90036=ORIENTED_EDGE ( 'NONE', *, *, #79020, .F. ) ;
#90037=DIRECTION ( 'NONE',  ( -0.7071067811865486830, -0.7071067811865464625, 0.000000000000000000 ) ) ;
#90038=ORIENTED_EDGE ( 'NONE', *, *, #110189, .T. ) ;
#90039=ORIENTED_EDGE ( 'NONE', *, *, #74001, .T. ) ;
#90040=EDGE_CURVE ( 'NONE', #21343, #141074, #65501, .T. ) ;
#90041=ORIENTED_EDGE ( 'NONE', *, *, #29130, .F. ) ;
#90043=ORIENTED_EDGE ( 'NONE', *, *, #119601, .F. ) ;
#90044=DIRECTION ( 'NONE',  ( -0.6830127018922180770, -0.6830127018922204085, -0.2588190451025213501 ) ) ;
#90046=FACE_OUTER_BOUND ( 'NONE', #7198, .T. ) ;
#90047=DIRECTION ( 'NONE',  ( 0.3543493200069163240, 0.000000000000000000, -0.9351131265310288487 ) ) ;
#90049=EDGE_CURVE ( 'NONE', #29880, #137064, #12497, .T. ) ;
#90050=ORIENTED_EDGE ( 'NONE', *, *, #83842, .F. ) ;
#90051=ADVANCED_FACE ( 'NONE', ( #78490 ), #121261, .T. ) ;
#90052=DIRECTION ( 'NONE',  ( -0.6830127018922181881, 0.6830127018922202975, -0.2588190451025214056 ) ) ;
#90053=CARTESIAN_POINT ( 'NONE',  ( -7.110173228882056051, -22.22500000000000497, 4.785647885939354751 ) ) ;
#90054=CARTESIAN_POINT ( 'NONE',  ( -11.99451991528749417, 28.92564299267946382, 4.000000000000000000 ) ) ;
#90055=LINE ( 'NONE', #113234, #64148 ) ;
#90057=CARTESIAN_POINT ( 'NONE',  ( -42.29974487139158157, -27.71228299555235708, 4.000000000000000000 ) ) ;
#90058=CARTESIAN_POINT ( 'NONE',  ( 27.18398860626900060, 28.73617430169806042, 5.000000000000000000 ) ) ;
#90060=LINE ( 'NONE', #89362, #132486 ) ;
#90061=CARTESIAN_POINT ( 'NONE',  ( 27.32816939922333432, -9.740707523384191546, 4.000000000000000000 ) ) ;
#90063=ORIENTED_EDGE ( 'NONE', *, *, #80980, .T. ) ;
#90065=LINE ( 'NONE', #69065, #143423 ) ;
#90066=ADVANCED_FACE ( 'NONE', ( #11042 ), #133589, .F. ) ;
#90068=VERTEX_POINT ( 'NONE', #119811 ) ;
#90069=LINE ( 'NONE', #911, #61790 ) ;
#90070=PLANE ( 'NONE',  #100123 ) ;
#90071=AXIS2_PLACEMENT_3D ( 'NONE', #97107, #41330, #86991 ) ;
#90073=EDGE_CURVE ( 'NONE', #135680, #66418, #110366, .T. ) ;
#90074=VERTEX_POINT ( 'NONE', #87218 ) ;
#90076=VECTOR ( 'NONE', #45054, 999.9999999999998863 ) ;
#90077=ORIENTED_EDGE ( 'NONE', *, *, #43880, .T. ) ;
#90079=VECTOR ( 'NONE', #977, 1000.000000000000000 ) ;
#90080=VECTOR ( 'NONE', #133727, 1000.000000000000227 ) ;
#90081=AXIS2_PLACEMENT_3D ( 'NONE', #140901, #61274, #60539 ) ;
#90082=LINE ( 'NONE', #12523, #75435 ) ;
#90086=ORIENTED_EDGE ( 'NONE', *, *, #89427, .F. ) ;
#90087=ADVANCED_FACE ( 'NONE', ( #20501 ), #66195, .F. ) ;
#90088=LINE ( 'NONE', #99522, #104371 ) ;
#90089=ORIENTED_EDGE ( 'NONE', *, *, #22878, .T. ) ;
#90092=DIRECTION ( 'NONE',  ( -0.6830127018922181881, 0.6830127018922202975, -0.2588190451025214056 ) ) ;
#90094=ADVANCED_FACE ( 'NONE', ( #98784 ), #111078, .F. ) ;
#90095=PLANE ( 'NONE',  #49195 ) ;
#90096=CARTESIAN_POINT ( 'NONE',  ( 36.08314806772909833, 21.75929247661549937, 7.311836541448132998 ) ) ;
#90097=DIRECTION ( 'NONE',  ( 0.7071067811865486830, -0.7071067811865464625, -0.000000000000000000 ) ) ;
#90098=AXIS2_PLACEMENT_3D ( 'NONE', #136389, #37078, #34239 ) ;
#90099=ORIENTED_EDGE ( 'NONE', *, *, #62067, .T. ) ;
#90100=CARTESIAN_POINT ( 'NONE',  ( 27.32816939922333432, -12.74070752338415247, 4.000000000000000000 ) ) ;
#90102=CARTESIAN_POINT ( 'NONE',  ( 2.994519915287485734, 28.92564299267940342, 4.000000000000000000 ) ) ;
#90103=CARTESIAN_POINT ( 'NONE',  ( -24.48921356237309510, -27.52281430457072631, 5.000000000000000000 ) ) ;
#90105=ORIENTED_EDGE ( 'NONE', *, *, #10585, .F. ) ;
#90106=ORIENTED_EDGE ( 'NONE', *, *, #61850, .F. ) ;
#90107=VECTOR ( 'NONE', #119434, 1000.000000000000000 ) ;
#90108=VECTOR ( 'NONE', #64892, 1000.000000000000227 ) ;
#90109=DIRECTION ( 'NONE',  ( -0.000000000000000000, 0.3543493200069153248, 0.9351131265310292928 ) ) ;
#90110=VERTEX_POINT ( 'NONE', #11769 ) ;
#90112=VECTOR ( 'NONE', #116822, 999.9999999999998863 ) ;
#90114=ORIENTED_EDGE ( 'NONE', *, *, #122223, .F. ) ;
#90115=CARTESIAN_POINT ( 'NONE',  ( 0.000000000000000000, 0.000000000000000000, 5.000000000000000000 ) ) ;
#90116=CARTESIAN_POINT ( 'NONE',  ( -57.18398860626899705, 28.73617430169827358, 5.000000000000000000 ) ) ;
#90117=VECTOR ( 'NONE', #117861, 1000.000000000000000 ) ;
#90119=DIRECTION ( 'NONE',  ( 0.7071067811865487940, -0.7071067811865463515, 0.000000000000000000 ) ) ;
#90120=VECTOR ( 'NONE', #20305, 1000.000000000000000 ) ;
#90121=FACE_BOUND ( 'NONE', #73795, .T. ) ;
#90122=CARTESIAN_POINT ( 'NONE',  ( -14.19331503651554272, 6.646281381260698673, 4.665372575888455664 ) ) ;
#90123=DIRECTION ( 'NONE',  ( 0.7071067811865487940, 0.7071067811865463515, -0.000000000000000000 ) ) ;
#90124=DIRECTION ( 'NONE',  ( -0.000000000000000000, 0.000000000000000000, 1.000000000000000000 ) ) ;
#90125=DIRECTION ( 'NONE',  ( 0.7071067811865486830, -0.7071067811865464625, -0.000000000000000000 ) ) ;
#90126=ORIENTED_EDGE ( 'NONE', *, *, #112601, .T. ) ;
#90129=CARTESIAN_POINT ( 'NONE',  ( 0.4892135623730947680, -27.52281430457055578, 5.000000000000000000 ) ) ;
#90131=ADVANCED_FACE ( 'NONE', ( #121960 ), #162, .F. ) ;
#90132=VERTEX_POINT ( 'NONE', #45181 ) ;
#90134=VERTEX_POINT ( 'NONE', #33581 ) ;
#90135=DIRECTION ( 'NONE',  ( 0.7071067811865487940, 0.7071067811865463515, -0.000000000000000000 ) ) ;
#90136=DIRECTION ( 'NONE',  ( -0.7071067811865487940, 0.7071067811865463515, 0.000000000000000000 ) ) ;
#90137=EDGE_CURVE ( 'NONE', #79543, #2861, #89357, .T. ) ;
#90138=VERTEX_POINT ( 'NONE', #53906 ) ;
#90139=FACE_OUTER_BOUND ( 'NONE', #130802, .T. ) ;
#90140=AXIS2_PLACEMENT_3D ( 'NONE', #134993, #12452, #121915 ) ;
#90141=ADVANCED_FACE ( 'NONE', ( #98099 ), #131444, .F. ) ;
#90142=EDGE_CURVE ( 'NONE', #57153, #11328, #15328, .T. ) ;
#90143=LINE ( 'NONE', #3126, #91196 ) ;
#90144=DIRECTION ( 'NONE',  ( 1.000000000000000000, 0.000000000000000000, 0.000000000000000000 ) ) ;
#90145=DIRECTION ( 'NONE',  ( 1.000000000000000000, 0.000000000000000000, 0.000000000000000000 ) ) ;
#90146=DIRECTION ( 'NONE',  ( -0.7071067811865486830, 0.7071067811865464625, 0.000000000000000000 ) ) ;
#90149=CARTESIAN_POINT ( 'NONE',  ( 12.29974487139158512, -27.71228299555214747, 4.000000000000000000 ) ) ;
#90150=EDGE_LOOP ( 'NONE', ( #55000, #97282, #67421, #32694 ) ) ;
#90151=VERTEX_POINT ( 'NONE', #16035 ) ;
#90152=DIRECTION ( 'NONE',  ( -0.000000000000000000, 0.000000000000000000, 1.000000000000000000 ) ) ;
#90153=ORIENTED_EDGE ( 'NONE', *, *, #4009, .T. ) ;
#90154=ORIENTED_EDGE ( 'NONE', *, *, #14812, .F. ) ;
#90155=EDGE_LOOP ( 'NONE', ( #93004, #113501, #53012, #131778 ) ) ;
#90156=EDGE_CURVE ( 'NONE', #120604, #111726, #113235, .T. ) ;
#90157=ADVANCED_FACE ( 'NONE', ( #136420 ), #58212, .F. ) ;
#90160=CARTESIAN_POINT ( 'NONE',  ( 16.17183060077635659, -14.24070752338414003, 4.000000000000000000 ) ) ;
#90161=ADVANCED_FACE ( 'NONE', ( #79956 ), #5166, .F. ) ;
#90162=DIRECTION ( 'NONE',  ( -0.7071067811865486830, -0.7071067811865464625, 0.000000000000000000 ) ) ;
#90164=LINE ( 'NONE', #67003, #30991 ) ;
#90165=ORIENTED_EDGE ( 'NONE', *, *, #38511, .F. ) ;
#90166=DIRECTION ( 'NONE',  ( -0.000000000000000000, 0.3543493200069153248, 0.9351131265310292928 ) ) ;
#90167=FACE_OUTER_BOUND ( 'NONE', #136724, .T. ) ;
#90168=CARTESIAN_POINT ( 'NONE',  ( 16.49999999999988987, 15.05218569542901186, 5.000000000000000000 ) ) ;
#90169=EDGE_CURVE ( 'NONE', #140659, #111351, #112536, .T. ) ;
#90170=DIRECTION ( 'NONE',  ( -0.7071067811865486830, -0.7071067811865464625, -0.000000000000000000 ) ) ;
#90172=VERTEX_POINT ( 'NONE', #92192 ) ;
#90174=CARTESIAN_POINT ( 'NONE',  ( 24.98911971346034022, -22.02621442084247505, 4.990779571109222879 ) ) ;
#90175=CARTESIAN_POINT ( 'NONE',  ( 0.000000000000000000, 0.000000000000000000, 5.000000000000000000 ) ) ;
#90176=EDGE_LOOP ( 'NONE', ( #79442, #130379, #84659, #36128 ) ) ;
#90177=CARTESIAN_POINT ( 'NONE',  ( 8.671830600776413434, -21.74070752338406365, 4.000000000000000000 ) ) ;
#90178=LINE ( 'NONE', #136531, #50222 ) ;
#90179=CARTESIAN_POINT ( 'NONE',  ( 34.92499999999998295, 0.006123077391964604210, 4.000000000000000000 ) ) ;
#90181=CARTESIAN_POINT ( 'NONE',  ( -5.206660635421487271, 21.75929247661549937, 4.998822639870708073 ) ) ;
#90182=EDGE_CURVE ( 'NONE', #45676, #11432, #26253, .T. ) ;
#90183=VECTOR ( 'NONE', #63292, 1000.000000000000000 ) ;
#90184=VECTOR ( 'NONE', #139630, 1000.000000000000000 ) ;
#90186=DIRECTION ( 'NONE',  ( -0.000000000000000000, -0.3543493200069152693, 0.9351131265310292928 ) ) ;
#90187=DIRECTION ( 'NONE',  ( -0.7071067811865486830, 0.7071067811865464625, 0.000000000000000000 ) ) ;
#90189=AXIS2_PLACEMENT_3D ( 'NONE', #70226, #115769, #135451 ) ;
#90190=CARTESIAN_POINT ( 'NONE',  ( -13.49999999999990763, -2.947814304570798960, 5.000000000000000000 ) ) ;
#90191=DIRECTION ( 'NONE',  ( -0.7071067811865487940, 0.7071067811865463515, -0.000000000000000000 ) ) ;
#90192=ORIENTED_EDGE ( 'NONE', *, *, #3389, .T. ) ;
#90193=EDGE_CURVE ( 'NONE', #69532, #49090, #24806, .T. ) ;
#90194=VERTEX_POINT ( 'NONE', #35004 ) ;
#90195=EDGE_CURVE ( 'NONE', #54251, #42897, #57471, .T. ) ;
#90196=DIRECTION ( 'NONE',  ( 0.6830127018922181881, 0.6830127018922202975, -0.2588190451025214056 ) ) ;
#90198=ADVANCED_FACE ( 'NONE', ( #101653 ), #2310, .F. ) ;
#90199=CARTESIAN_POINT ( 'NONE',  ( 0.000000000000000000, 21.72500000000000142, 4.500000000000000888 ) ) ;
#90200=LINE ( 'NONE', #133724, #122286 ) ;
#90201=EDGE_LOOP ( 'NONE', ( #118268, #79728, #22118, #4383 ) ) ;
#90204=CARTESIAN_POINT ( 'NONE',  ( 5.999999999999956479, -19.22509904557635707, 1.855685503482192189 ) ) ;
#90205=FACE_OUTER_BOUND ( 'NONE', #122437, .T. ) ;
#90206=VERTEX_POINT ( 'NONE', #3050 ) ;
#90208=DIRECTION ( 'NONE',  ( 0.7071067811865487940, 0.7071067811865463515, 0.000000000000000000 ) ) ;
#90209=AXIS2_PLACEMENT_3D ( 'NONE', #32671, #20325, #21781 ) ;
#90210=AXIS2_PLACEMENT_3D ( 'NONE', #132056, #55202, #111721 ) ;
#90211=CARTESIAN_POINT ( 'NONE',  ( -0.2997448713915885632, -27.71228299555206220, 4.000000000000000000 ) ) ;
#90213=( BOUNDED_CURVE ( )  B_SPLINE_CURVE ( 3, ( #85402, #94144, #8526, #138381 ),
 .UNSPECIFIED., .F., .T. ) 
 B_SPLINE_CURVE_WITH_KNOTS ( ( 4, 4 ),
 ( 1.208578181583236821, 1.359146454359470901 ),
 .UNSPECIFIED. ) 
 CURVE ( )  GEOMETRIC_REPRESENTATION_ITEM ( )  RATIONAL_B_SPLINE_CURVE ( ( 1.000000000000000000, 0.9981116584018945304, 0.9981116584018945304, 1.000000000000000000 ) ) 
 REPRESENTATION_ITEM ( '' )  );
#90214=LINE ( 'NONE', #57617, #83527 ) ;
#90216=CARTESIAN_POINT ( 'NONE',  ( 25.82816939922335209, 12.75929247661558819, 4.000000000000000000 ) ) ;
#90217=VERTEX_POINT ( 'NONE', #124127 ) ;
#90218=DIRECTION ( 'NONE',  ( 0.7071067811865487940, 0.7071067811865463515, 0.000000000000000000 ) ) ;
#90219=VERTEX_POINT ( 'NONE', #46628 ) ;
#90221=VECTOR ( 'NONE', #9484, 1000.000000000000227 ) ;
#90223=AXIS2_PLACEMENT_3D ( 'NONE', #24438, #125186, #46968 ) ;
#90224=CARTESIAN_POINT ( 'NONE',  ( -57.29974487139158157, -27.71228299555246011, 4.000000000000000000 ) ) ;
#90225=LINE ( 'NONE', #111247, #44270 ) ;
#90226=CARTESIAN_POINT ( 'NONE',  ( 19.74845587132413272, -11.24070752338416135, 10.39518518046004658 ) ) ;
#90227=LINE ( 'NONE', #101823, #104317 ) ;
#90229=ORIENTED_EDGE ( 'NONE', *, *, #63335, .F. ) ;
#90230=EDGE_LOOP ( 'NONE', ( #107063, #43152, #76370, #17313 ) ) ;
#90231=DIRECTION ( 'NONE',  ( -0.7071067811865486830, -0.7071067811865464625, 0.000000000000000000 ) ) ;
#90233=AXIS2_PLACEMENT_3D ( 'NONE', #127898, #70678, #59784 ) ;
#90234=CARTESIAN_POINT ( 'NONE',  ( -15.79289321881334551, 12.75929247661558641, 5.000000000000000000 ) ) ;
#90235=LINE ( 'NONE', #68522, #122151 ) ;
#90237=DIRECTION ( 'NONE',  ( 0.6830127018922180770, -0.6830127018922204085, -0.2588190451025213501 ) ) ;
#90238=DIRECTION ( 'NONE',  ( 0.6830127018922181881, 0.6830127018922202975, -0.2588190451025214056 ) ) ;
#90239=ORIENTED_EDGE ( 'NONE', *, *, #36800, .F. ) ;
#90241=FACE_OUTER_BOUND ( 'NONE', #104193, .T. ) ;
#90243=LINE ( 'NONE', #35907, #60151 ) ;
#90245=AXIS2_PLACEMENT_3D ( 'NONE', #90971, #27827, #15486 ) ;
#90246=ORIENTED_EDGE ( 'NONE', *, *, #2802, .T. ) ;
#90247=PLANE ( 'NONE',  #35270 ) ;
#90250=ORIENTED_EDGE ( 'NONE', *, *, #17937, .T. ) ;
#90252=AXIS2_PLACEMENT_3D ( 'NONE', #87147, #6678, #84323 ) ;
#90254=CARTESIAN_POINT ( 'NONE',  ( -31.49999999999978684, 3.073033219394599058, -6.593910359671041554 ) ) ;
#90255=LINE ( 'NONE', #79447, #53258 ) ;
#90256=EDGE_CURVE ( 'NONE', #142977, #42748, #135043, .T. ) ;
#90259=EDGE_CURVE ( 'NONE', #135515, #135619, #142370, .T. ) ;
#90260=CARTESIAN_POINT ( 'NONE',  ( 59.99451991528749772, 28.92564299267980132, 4.000000000000000000 ) ) ;
#90261=DIRECTION ( 'NONE',  ( -0.7071067811865486830, -0.7071067811865464625, 0.000000000000000000 ) ) ;
#90262=LINE ( 'NONE', #78688, #95736 ) ;
#90264=ORIENTED_EDGE ( 'NONE', *, *, #53526, .T. ) ;
#90265=ORIENTED_EDGE ( 'NONE', *, *, #106962, .T. ) ;
#90267=ORIENTED_EDGE ( 'NONE', *, *, #34099, .T. ) ;
#90268=EDGE_CURVE ( 'NONE', #24066, #116804, #50855, .T. ) ;
#90269=PLANE ( 'NONE',  #38353 ) ;
#90270=DIRECTION ( 'NONE',  ( 0.7071067811865486830, -0.7071067811865464625, -0.000000000000000000 ) ) ;
#90271=LINE ( 'NONE', #2530, #84975 ) ;
#90272=DIRECTION ( 'NONE',  ( -0.7071067811865486830, -0.7071067811865464625, 0.000000000000000000 ) ) ;
#90274=ORIENTED_EDGE ( 'NONE', *, *, #71290, .F. ) ;
#90276=DIRECTION ( 'NONE',  ( -0.3543493200069162685, -0.000000000000000000, -0.9351131265310288487 ) ) ;
#90278=EDGE_CURVE ( 'NONE', #53667, #132228, #137880, .T. ) ;
#90279=VECTOR ( 'NONE', #7617, 999.9999999999998863 ) ;
#90280=ORIENTED_EDGE ( 'NONE', *, *, #114142, .T. ) ;
#90281=LINE ( 'NONE', #114864, #7397 ) ;
#90282=DIRECTION ( 'NONE',  ( 0.6830127018922180770, -0.6830127018922204085, -0.2588190451025213501 ) ) ;
#90283=CARTESIAN_POINT ( 'NONE',  ( 13.49999999999990052, 22.22500000000000142, 4.362957392718788796 ) ) ;
#90284=VECTOR ( 'NONE', #84828, 999.9999999999998863 ) ;
#90285=EDGE_CURVE ( 'NONE', #142977, #67716, #84227, .T. ) ;
#90286=VECTOR ( 'NONE', #10835, 1000.000000000000227 ) ;
#90287=VECTOR ( 'NONE', #105854, 999.9999999999998863 ) ;
#90288=EDGE_CURVE ( 'NONE', #55364, #76579, #110028, .T. ) ;
#90289=ORIENTED_EDGE ( 'NONE', *, *, #89769, .T. ) ;
#90290=FACE_BOUND ( 'NONE', #126399, .T. ) ;
#90292=CARTESIAN_POINT ( 'NONE',  ( 36.29974487139159578, -27.71228299555231445, 4.000000000000000000 ) ) ;
#90294=VECTOR ( 'NONE', #46802, 1000.000000000000000 ) ;
#90295=LINE ( 'NONE', #3951, #87426 ) ;
#90296=DIRECTION ( 'NONE',  ( -0.7071067811865487940, 0.7071067811865463515, -0.000000000000000000 ) ) ;
#90298=ORIENTED_EDGE ( 'NONE', *, *, #98675, .T. ) ;
#90302=DIRECTION ( 'NONE',  ( -0.3543493200069162685, -0.000000000000000000, -0.9351131265310288487 ) ) ;
#90303=ORIENTED_EDGE ( 'NONE', *, *, #141389, .T. ) ;
#90304=ADVANCED_FACE ( 'NONE', ( #120914 ), #128424, .F. ) ;
#90305=VECTOR ( 'NONE', #86118, 1000.000000000000227 ) ;
#90306=VECTOR ( 'NONE', #55679, 1000.000000000000000 ) ;
#90307=DIRECTION ( 'NONE',  ( -0.7071067811865487940, 0.7071067811865463515, 0.000000000000000000 ) ) ;
#90308=CARTESIAN_POINT ( 'NONE',  ( 12.48921356237309155, -27.52281430457064104, 5.000000000000000000 ) ) ;
#90309=EDGE_CURVE ( 'NONE', #116082, #135321, #97742, .T. ) ;
#90310=EDGE_CURVE ( 'NONE', #90465, #37645, #16792, .T. ) ;
#90311=AXIS2_PLACEMENT_3D ( 'NONE', #117007, #127166, #6067 ) ;
#90312=LINE ( 'NONE', #25046, #91081 ) ;
#90314=DIRECTION ( 'NONE',  ( 0.3543493200069162685, -0.000000000000000000, -0.9351131265310288487 ) ) ;
#90315=CARTESIAN_POINT ( 'NONE',  ( -54.48921356237310221, -27.52281430457093236, 5.000000000000000000 ) ) ;
#90316=PLANE ( 'NONE',  #133455 ) ;
#90317=DIRECTION ( 'NONE',  ( 0.7071067811865487940, 0.7071067811865463515, 0.000000000000000000 ) ) ;
#90320=LINE ( 'NONE', #80198, #139401 ) ;
#90321=ORIENTED_EDGE ( 'NONE', *, *, #29127, .T. ) ;
#90326=ORIENTED_EDGE ( 'NONE', *, *, #91183, .T. ) ;
#90327=ORIENTED_EDGE ( 'NONE', *, *, #54560, .F. ) ;
#90330=EDGE_CURVE ( 'NONE', #37842, #2427, #108572, .T. ) ;
#90331=EDGE_LOOP ( 'NONE', ( #111199, #27361, #58921, #91858 ) ) ;
#90334=DIRECTION ( 'NONE',  ( -0.000000000000000000, -0.3543493200069152693, 0.9351131265310292928 ) ) ;
#90335=VECTOR ( 'NONE', #142395, 1000.000000000000000 ) ;
#90338=DIRECTION ( 'NONE',  ( 0.000000000000000000, 0.000000000000000000, -1.000000000000000000 ) ) ;
#90339=EDGE_CURVE ( 'NONE', #74056, #115521, #105226, .T. ) ;
#90340=VERTEX_POINT ( 'NONE', #141986 ) ;
#90342=ORIENTED_EDGE ( 'NONE', *, *, #68787, .T. ) ;
#90343=CARTESIAN_POINT ( 'NONE',  ( 19.49999999999985789, -16.53360074219757436, 5.000000000000000000 ) ) ;
#90344=VECTOR ( 'NONE', #74028, 1000.000000000000227 ) ;
#90345=EDGE_CURVE ( 'NONE', #92829, #108854, #9254, .T. ) ;
#90346=DIRECTION ( 'NONE',  ( 0.7071067811865486830, -0.7071067811865464625, -0.000000000000000000 ) ) ;
#90347=ORIENTED_EDGE ( 'NONE', *, *, #8204, .F. ) ;
#90348=CARTESIAN_POINT ( 'NONE',  ( -21.22572773465412865, 22.22500000000000142, -0.1911663670286917194 ) ) ;
#90349=DIRECTION ( 'NONE',  ( -0.3543493200069162685, -0.000000000000000000, -0.9351131265310288487 ) ) ;
#90350=LINE ( 'NONE', #112125, #56745 ) ;
#90351=VERTEX_POINT ( 'NONE', #53531 ) ;
#90352=LINE ( 'NONE', #123727, #8704 ) ;
#90353=ORIENTED_EDGE ( 'NONE', *, *, #83805, .T. ) ;
#90354=ORIENTED_EDGE ( 'NONE', *, *, #83521, .T. ) ;
#90355=ORIENTED_EDGE ( 'NONE', *, *, #110445, .T. ) ;
#90356=DIRECTION ( 'NONE',  ( -0.7071067811865486830, 0.7071067811865464625, 0.000000000000000000 ) ) ;
#90359=CARTESIAN_POINT ( 'NONE',  ( -33.18398860626899705, 28.73617430169810305, 5.000000000000000000 ) ) ;
#90360=DIRECTION ( 'NONE',  ( -0.7071067811865486830, -0.7071067811865464625, 0.000000000000000000 ) ) ;
#90361=PLANE ( 'NONE',  #90582 ) ;
#90363=VECTOR ( 'NONE', #42483, 1000.000000000000227 ) ;
#90365=EDGE_CURVE ( 'NONE', #31098, #35930, #105914, .T. ) ;
#90368=CARTESIAN_POINT ( 'NONE',  ( -21.18398860626899349, 28.73617430169802134, 5.000000000000000000 ) ) ;
#90369=DIRECTION ( 'NONE',  ( -0.000000000000000000, 0.000000000000000000, 1.000000000000000000 ) ) ;
#90370=( BOUNDED_CURVE ( )  B_SPLINE_CURVE ( 3, ( #18795, #30408, #137757, #29667 ),
 .UNSPECIFIED., .F., .T. ) 
 B_SPLINE_CURVE_WITH_KNOTS ( ( 4, 4 ),
 ( 1.864375635226932282, 1.933014472006565176 ),
 .UNSPECIFIED. ) 
 CURVE ( )  GEOMETRIC_REPRESENTATION_ITEM ( )  RATIONAL_B_SPLINE_CURVE ( ( 1.000000000000000000, 0.9996074310407762065, 0.9996074310407762065, 1.000000000000000000 ) ) 
 REPRESENTATION_ITEM ( '' )  );
#90371=CARTESIAN_POINT ( 'NONE',  ( 19.17183060077633172, -17.24070752338411339, 4.000000000000000000 ) ) ;
#90373=ORIENTED_EDGE ( 'NONE', *, *, #16436, .F. ) ;
#90375=VERTEX_POINT ( 'NONE', #66550 ) ;
#90376=LINE ( 'NONE', #2638, #99632 ) ;
#90377=DIRECTION ( 'NONE',  ( 0.7071067811865486830, -0.7071067811865464625, -0.000000000000000000 ) ) ;
#90379=VECTOR ( 'NONE', #27260, 1000.000000000000000 ) ;
#90380=EDGE_CURVE ( 'NONE', #92320, #127894, #57838, .T. ) ;
#90381=PLANE ( 'NONE',  #73707 ) ;
#90382=CARTESIAN_POINT ( 'NONE',  ( -25.49999999999982236, 1.030536316426491128, -5.498701923753738896 ) ) ;
#90383=VECTOR ( 'NONE', #33311, 1000.000000000000227 ) ;
#90384=VECTOR ( 'NONE', #28615, 1000.000000000000227 ) ;
#90386=LINE ( 'NONE', #12811, #45653 ) ;
#90387=LINE ( 'NONE', #125159, #333 ) ;
#90388=CARTESIAN_POINT ( 'NONE',  ( 13.49999999999990585, -10.53360074219763121, 5.000000000000000000 ) ) ;
#90389=DIRECTION ( 'NONE',  ( -0.000000000000000000, 0.000000000000000000, 1.000000000000000000 ) ) ;
#90390=ORIENTED_EDGE ( 'NONE', *, *, #78922, .T. ) ;
#90391=VECTOR ( 'NONE', #126038, 1000.000000000000227 ) ;
#90392=VECTOR ( 'NONE', #125172, 999.9999999999998863 ) ;
#90393=VECTOR ( 'NONE', #81859, 999.9999999999998863 ) ;
#90395=ORIENTED_EDGE ( 'NONE', *, *, #93138, .T. ) ;
#90397=CARTESIAN_POINT ( 'NONE',  ( 5.292893218813418343, -3.740707523384243505, 5.000000000000000000 ) ) ;
#90398=CARTESIAN_POINT ( 'NONE',  ( -34.49999999999975842, 15.05432934483078533, 4.994342998332167660 ) ) ;
#90399=VERTEX_POINT ( 'NONE', #68023 ) ;
#90400=LINE ( 'NONE', #134647, #91207 ) ;
#90401=VERTEX_POINT ( 'NONE', #133251 ) ;
#90403=ORIENTED_EDGE ( 'NONE', *, *, #51989, .T. ) ;
#90404=FACE_OUTER_BOUND ( 'NONE', #98794, .T. ) ;
#90406=ORIENTED_EDGE ( 'NONE', *, *, #8217, .T. ) ;
#90407=( BOUNDED_CURVE ( )  B_SPLINE_CURVE ( 3, ( #42789, #76853, #121028, #31889 ),
 .UNSPECIFIED., .F., .F. ) 
 B_SPLINE_CURVE_WITH_KNOTS ( ( 4, 4 ),
 ( 5.143245962375958769, 6.645403452391247079 ),
 .UNSPECIFIED. ) 
 CURVE ( )  GEOMETRIC_REPRESENTATION_ITEM ( )  RATIONAL_B_SPLINE_CURVE ( ( 1.000000000000000000, 0.8206354192515226131, 0.8206354192515226131, 1.000000000000000000 ) ) 
 REPRESENTATION_ITEM ( '' )  );
#90408=CARTESIAN_POINT ( 'NONE',  ( -59.99451991528749772, 28.92564299267980132, 4.000000000000000000 ) ) ;
#90410=DIRECTION ( 'NONE',  ( 0.7071067811865487940, -0.7071067811865463515, 0.000000000000000000 ) ) ;
#90411=PLANE ( 'NONE',  #90223 ) ;
#90412=ORIENTED_EDGE ( 'NONE', *, *, #127140, .T. ) ;
#90414=LINE ( 'NONE', #24441, #72762 ) ;
#90415=EDGE_CURVE ( 'NONE', #74158, #141302, #77453, .T. ) ;
#90418=LINE ( 'NONE', #134666, #109299 ) ;
#90419=AXIS2_PLACEMENT_3D ( 'NONE', #50630, #17959, #5668 ) ;
#90421=LINE ( 'NONE', #79606, #29269 ) ;
#90422=VERTEX_POINT ( 'NONE', #22997 ) ;
#90424=CARTESIAN_POINT ( 'NONE',  ( 8.816011393731004731, 28.73617430169781173, 5.000000000000000000 ) ) ;
#90425=ORIENTED_EDGE ( 'NONE', *, *, #88874, .F. ) ;
#90429=CARTESIAN_POINT ( 'NONE',  ( 29.67183060077626422, -21.74070752338406010, 4.000000000000000000 ) ) ;
#90430=CARTESIAN_POINT ( 'NONE',  ( -34.75611968250420603, -7.294349301475856251, 4.955485411084898040 ) ) ;
#90433=VECTOR ( 'NONE', #54065, 1000.000000000000000 ) ;
#90434=CARTESIAN_POINT ( 'NONE',  ( 0.000000000000000000, 0.000000000000000000, 5.000000000000000000 ) ) ;
#90435=CARTESIAN_POINT ( 'NONE',  ( -34.75611968250420603, -13.29434930147579941, 4.955485411084898040 ) ) ;
#90436=EDGE_CURVE ( 'NONE', #32991, #69078, #122320, .T. ) ;
#90437=DIRECTION ( 'NONE',  ( 0.6830127018922181881, 0.6830127018922202975, -0.2588190451025214056 ) ) ;
#90438=ORIENTED_EDGE ( 'NONE', *, *, #113604, .T. ) ;
#90439=CARTESIAN_POINT ( 'NONE',  ( 24.79593897580385331, 4.791522900035168675, 4.000000000000000000 ) ) ;
#90441=ADVANCED_FACE ( 'NONE', ( #1945 ), #132556, .F. ) ;
#90442=VECTOR ( 'NONE', #143164, 1000.000000000000000 ) ;
#90443=DIRECTION ( 'NONE',  ( 1.000000000000000000, 0.000000000000000000, 0.000000000000000000 ) ) ;
#90444=LINE ( 'NONE', #80309, #40537 ) ;
#90445=ORIENTED_EDGE ( 'NONE', *, *, #45655, .T. ) ;
#90446=DIRECTION ( 'NONE',  ( -1.000000000000000000, 0.000000000000000000, 0.000000000000000000 ) ) ;
#90449=LINE ( 'NONE', #562, #57244 ) ;
#90450=LINE ( 'NONE', #137533, #128017 ) ;
#90451=ADVANCED_FACE ( 'NONE', ( #46253 ), #1256, .T. ) ;
#90452=EDGE_CURVE ( 'NONE', #129956, #85957, #550, .T. ) ;
#90455=ORIENTED_EDGE ( 'NONE', *, *, #63621, .F. ) ;
#90459=EDGE_CURVE ( 'NONE', #39260, #41530, #123802, .T. ) ;
#90460=DIRECTION ( 'NONE',  ( -0.7071067811865486830, -0.7071067811865464625, 0.000000000000000000 ) ) ;
#90461=LINE ( 'NONE', #55707, #13246 ) ;
#90462=VECTOR ( 'NONE', #75463, 1000.000000000000227 ) ;
#90463=FACE_OUTER_BOUND ( 'NONE', #63625, .T. ) ;
#90464=FACE_OUTER_BOUND ( 'NONE', #108074, .T. ) ;
#90465=VERTEX_POINT ( 'NONE', #68704 ) ;
#90467=CARTESIAN_POINT ( 'NONE',  ( -11.99451991528749417, 28.92564299267946382, 4.000000000000000000 ) ) ;
#90468=ADVANCED_FACE ( 'NONE', ( #99137 ), #110722, .F. ) ;
#90471=VERTEX_POINT ( 'NONE', #55685 ) ;
#90473=ADVANCED_FACE ( 'NONE', ( #115727 ), #27318, .F. ) ;
#90474=CARTESIAN_POINT ( 'NONE',  ( 2.292893218813448986, -12.74070752338415247, 5.000000000000000000 ) ) ;
#90475=VECTOR ( 'NONE', #30099, 1000.000000000000000 ) ;
#90476=EDGE_CURVE ( 'NONE', #79668, #99063, #5563, .T. ) ;
#90478=EDGE_LOOP ( 'NONE', ( #61488, #61966, #133378, #110950 ) ) ;
#90479=CARTESIAN_POINT ( 'NONE',  ( -4.499999999999976019, -8.568876922607730151, 4.000000000000000000 ) ) ;
#90481=CARTESIAN_POINT ( 'NONE',  ( 19.49999999999986500, -4.533600742197692490, 5.000000000000000000 ) ) ;
#90482=EDGE_CURVE ( 'NONE', #123934, #86133, #70182, .T. ) ;
#90483=AXIS2_PLACEMENT_3D ( 'NONE', #27649, #60321, #103765 ) ;
#90484=VECTOR ( 'NONE', #73278, 1000.000000000000000 ) ;
#90485=FACE_OUTER_BOUND ( 'NONE', #90728, .T. ) ;
#90486=DIRECTION ( 'NONE',  ( 1.000000000000000000, 0.000000000000000000, 0.000000000000000000 ) ) ;
#90487=DIRECTION ( 'NONE',  ( 0.6830127018922181881, 0.6830127018922202975, -0.2588190451025214056 ) ) ;
#90488=ORIENTED_EDGE ( 'NONE', *, *, #70403, .F. ) ;
#90490=CARTESIAN_POINT ( 'NONE',  ( 0.000000000000000000, 0.000000000000000000, 5.000000000000000000 ) ) ;
#90493=ADVANCED_FACE ( 'NONE', ( #115021 ), #70868, .F. ) ;
#90495=VECTOR ( 'NONE', #101922, 1000.000000000000227 ) ;
#90496=EDGE_CURVE ( 'NONE', #128364, #25807, #137541, .T. ) ;
#90497=VECTOR ( 'NONE', #93329, 999.9999999999998863 ) ;
#90498=LINE ( 'NONE', #14357, #93748 ) ;
#90499=EDGE_LOOP ( 'NONE', ( #76812, #79240, #29748, #130210 ) ) ;
#90500=PLANE ( 'NONE',  #106096 ) ;
#90501=CARTESIAN_POINT ( 'NONE',  ( -17.90332935812583770, -2.240707523384257716, 15.26439735382748353 ) ) ;
#90502=ADVANCED_FACE ( 'NONE', ( #128101 ), #15016, .T. ) ;
#90503=DIRECTION ( 'NONE',  ( 0.7071067811865486830, -0.7071067811865464625, -0.000000000000000000 ) ) ;
#90504=VECTOR ( 'NONE', #7436, 1000.000000000000000 ) ;
#90506=VECTOR ( 'NONE', #114623, 1000.000000000000000 ) ;
#90508=LINE ( 'NONE', #104934, #35192 ) ;
#90509=ORIENTED_EDGE ( 'NONE', *, *, #116309, .F. ) ;
#90510=ADVANCED_FACE ( 'NONE', ( #60725 ), #83895, .F. ) ;
#90511=VECTOR ( 'NONE', #120638, 1000.000000000000000 ) ;
#90512=DIRECTION ( 'NONE',  ( 0.000000000000000000, 0.000000000000000000, -1.000000000000000000 ) ) ;
#90513=ORIENTED_EDGE ( 'NONE', *, *, #3443, .T. ) ;
#90514=DIRECTION ( 'NONE',  ( 0.7071067811865487940, 0.7071067811865463515, 0.000000000000000000 ) ) ;
#90515=ORIENTED_EDGE ( 'NONE', *, *, #80792, .F. ) ;
#90517=ORIENTED_EDGE ( 'NONE', *, *, #97128, .F. ) ;
#90518=LINE ( 'NONE', #93362, #34332 ) ;
#90519=EDGE_LOOP ( 'NONE', ( #96912, #94736, #42808, #35078 ) ) ;
#90520=ORIENTED_EDGE ( 'NONE', *, *, #84339, .F. ) ;
#90522=VERTEX_POINT ( 'NONE', #4091 ) ;
#90525=CARTESIAN_POINT ( 'NONE',  ( 33.48921356237309510, -27.52281430457078670, 5.000000000000000000 ) ) ;
#90527=PLANE ( 'NONE',  #19586 ) ;
#90530=FACE_OUTER_BOUND ( 'NONE', #47852, .T. ) ;
#90532=LINE ( 'NONE', #91937, #134675 ) ;
#90533=AXIS2_PLACEMENT_3D ( 'NONE', #120864, #109287, #85380 ) ;
#90534=ADVANCED_FACE ( 'NONE', ( #17181 ), #136810, .F. ) ;
#90536=VECTOR ( 'NONE', #8939, 1000.000000000000000 ) ;
#90537=DIRECTION ( 'NONE',  ( -0.000000000000000000, -0.3543493200069152693, 0.9351131265310292928 ) ) ;
#90538=ORIENTED_EDGE ( 'NONE', *, *, #70201, .F. ) ;
#90539=VECTOR ( 'NONE', #19131, 1000.000000000000000 ) ;
#90541=CARTESIAN_POINT ( 'NONE',  ( -9.299744871391588674, -27.71228299555212971, 4.000000000000000000 ) ) ;
#90542=EDGE_LOOP ( 'NONE', ( #16845, #60869, #73091, #64934 ) ) ;
#90543=AXIS2_PLACEMENT_3D ( 'NONE', #141896, #109234, #9160 ) ;
#90544=ORIENTED_EDGE ( 'NONE', *, *, #21206, .T. ) ;
#90545=CARTESIAN_POINT ( 'NONE',  ( 15.70701326429294475, -21.74070752338405654, 4.999753212805220670 ) ) ;
#90546=ORIENTED_EDGE ( 'NONE', *, *, #123884, .T. ) ;
#90547=VECTOR ( 'NONE', #135703, 999.9999999999998863 ) ;
#90548=LINE ( 'NONE', #23860, #109250 ) ;
#90549=PLANE ( 'NONE',  #13125 ) ;
#90550=VECTOR ( 'NONE', #134270, 999.9999999999998863 ) ;
#90551=CARTESIAN_POINT ( 'NONE',  ( -33.48921356237309510, -27.52281430457078670, 5.000000000000000000 ) ) ;
#90552=CARTESIAN_POINT ( 'NONE',  ( -32.24139925780183091, 21.72499999999999432, 5.000000000000000000 ) ) ;
#90554=ORIENTED_EDGE ( 'NONE', *, *, #17488, .F. ) ;
#90555=LINE ( 'NONE', #136182, #46434 ) ;
#90556=ORIENTED_EDGE ( 'NONE', *, *, #29664, .F. ) ;
#90557=DIRECTION ( 'NONE',  ( -0.7071067811865486830, -0.7071067811865464625, -0.000000000000000000 ) ) ;
#90558=EDGE_CURVE ( 'NONE', #126051, #121499, #61443, .T. ) ;
#90559=VECTOR ( 'NONE', #122664, 999.9999999999998863 ) ;
#90561=VERTEX_POINT ( 'NONE', #107734 ) ;
#90563=CARTESIAN_POINT ( 'NONE',  ( 60.48921356237309510, -27.52281430457097500, 5.000000000000000000 ) ) ;
#90566=ORIENTED_EDGE ( 'NONE', *, *, #293, .F. ) ;
#90567=VECTOR ( 'NONE', #138954, 1000.000000000000000 ) ;
#90568=ORIENTED_EDGE ( 'NONE', *, *, #126365, .F. ) ;
#90569=DIRECTION ( 'NONE',  ( -0.7071067811865487940, 0.7071067811865463515, 0.000000000000000000 ) ) ;
#90570=DIRECTION ( 'NONE',  ( -0.000000000000000000, -0.3543493200069152693, 0.9351131265310292928 ) ) ;
#90571=FACE_OUTER_BOUND ( 'NONE', #40000, .T. ) ;
#90573=FACE_OUTER_BOUND ( 'NONE', #86574, .T. ) ;
#90575=ORIENTED_EDGE ( 'NONE', *, *, #71820, .F. ) ;
#90579=PLANE ( 'NONE',  #100094 ) ;
#90580=VECTOR ( 'NONE', #110036, 1000.000000000000000 ) ;
#90581=ORIENTED_EDGE ( 'NONE', *, *, #116649, .F. ) ;
#90582=AXIS2_PLACEMENT_3D ( 'NONE', #81668, #38147, #69349 ) ;
#90584=ORIENTED_EDGE ( 'NONE', *, *, #54373, .F. ) ;
#90585=VERTEX_POINT ( 'NONE', #84589 ) ;
#90586=ORIENTED_EDGE ( 'NONE', *, *, #33248, .F. ) ;
#90587=EDGE_CURVE ( 'NONE', #118712, #126622, #52648, .T. ) ;
#90589=FACE_OUTER_BOUND ( 'NONE', #1246, .T. ) ;
#90590=CIRCLE ( 'NONE', #116009, 5.968999999999998529 ) ;
#90591=VERTEX_POINT ( 'NONE', #74432 ) ;
#90592=ORIENTED_EDGE ( 'NONE', *, *, #94086, .T. ) ;
#90593=LINE ( 'NONE', #122475, #66024 ) ;
#90594=LINE ( 'NONE', #34789, #41611 ) ;
#90596=LINE ( 'NONE', #47837, #32072 ) ;
#90597=DIRECTION ( 'NONE',  ( -0.6830127018922180770, -0.6830127018922204085, -0.2588190451025213501 ) ) ;
#90598=DIRECTION ( 'NONE',  ( 0.000000000000000000, 0.000000000000000000, -1.000000000000000000 ) ) ;
#90599=DIRECTION ( 'NONE',  ( -0.7071067811865486830, -0.7071067811865464625, -0.000000000000000000 ) ) ;
#90600=LINE ( 'NONE', #135539, #120104 ) ;
#90604=VECTOR ( 'NONE', #73272, 999.9999999999998863 ) ;
#90605=DIRECTION ( 'NONE',  ( 0.7071067811865487940, 0.7071067811865463515, 0.000000000000000000 ) ) ;
#90606=DIRECTION ( 'NONE',  ( 0.7071067811865487940, 0.7071067811865463515, 0.000000000000000000 ) ) ;
#90607=ORIENTED_EDGE ( 'NONE', *, *, #73150, .F. ) ;
#90608=ORIENTED_EDGE ( 'NONE', *, *, #77390, .T. ) ;
#90611=VECTOR ( 'NONE', #101889, 1000.000000000000000 ) ;
#90612=EDGE_LOOP ( 'NONE', ( #125062, #113107, #77680, #130566 ) ) ;
#90613=ORIENTED_EDGE ( 'NONE', *, *, #107117, .F. ) ;
#90614=ORIENTED_EDGE ( 'NONE', *, *, #110621, .T. ) ;
#90615=EDGE_CURVE ( 'NONE', #96207, #80484, #32343, .T. ) ;
#90616=LINE ( 'NONE', #123963, #13254 ) ;
#90617=DIRECTION ( 'NONE',  ( 0.6830127018922180770, -0.6830127018922204085, -0.2588190451025213501 ) ) ;
#90618=VECTOR ( 'NONE', #42803, 999.9999999999998863 ) ;
#90619=AXIS2_PLACEMENT_3D ( 'NONE', #100929, #78481, #44450 ) ;
#90620=AXIS2_PLACEMENT_3D ( 'NONE', #128901, #87556, #85390 ) ;
#90623=ORIENTED_EDGE ( 'NONE', *, *, #38939, .T. ) ;
#90624=DIRECTION ( 'NONE',  ( -0.7071067811865486830, -0.7071067811865464625, 0.000000000000000000 ) ) ;
#90625=AXIS2_PLACEMENT_3D ( 'NONE', #59548, #70449, #56716 ) ;
#90626=PLANE ( 'NONE',  #95100 ) ;
#90627=DIRECTION ( 'NONE',  ( -0.7071067811865486830, -0.7071067811865464625, -0.000000000000000000 ) ) ;
#90628=CARTESIAN_POINT ( 'NONE',  ( -7.499999999999944045, -19.53360074219753884, 5.000000000000000000 ) ) ;
#90629=EDGE_CURVE ( 'NONE', #93458, #84994, #62845, .T. ) ;
#90630=EDGE_CURVE ( 'NONE', #18836, #42793, #120758, .T. ) ;
#90631=LINE ( 'NONE', #47173, #48845 ) ;
#90632=DIRECTION ( 'NONE',  ( -0.7071067811865486830, -0.7071067811865464625, 0.000000000000000000 ) ) ;
#90634=VECTOR ( 'NONE', #142354, 1000.000000000000114 ) ;
#90635=FACE_OUTER_BOUND ( 'NONE', #66436, .T. ) ;
#90636=LINE ( 'NONE', #123974, #66130 ) ;
#90638=CARTESIAN_POINT ( 'NONE',  ( 45.18398860626900415, 28.73617430169818832, 5.000000000000000000 ) ) ;
#90639=CARTESIAN_POINT ( 'NONE',  ( 26.99451991528749417, 28.92564299267956685, 4.000000000000000000 ) ) ;
#90640=CARTESIAN_POINT ( 'NONE',  ( -20.48334561358941386, 22.22500000000000142, 4.500000000000000888 ) ) ;
#90641=EDGE_CURVE ( 'NONE', #33213, #91632, #29465, .T. ) ;
#90642=EDGE_CURVE ( 'NONE', #31547, #94901, #63575, .T. ) ;
#90643=ORIENTED_EDGE ( 'NONE', *, *, #5022, .F. ) ;
#90644=EDGE_LOOP ( 'NONE', ( #10454, #29985, #131296, #80375 ) ) ;
#90646=ADVANCED_FACE ( 'NONE', ( #96834 ), #54818, .F. ) ;
#90647=VERTEX_POINT ( 'NONE', #128786 ) ;
#90648=VECTOR ( 'NONE', #128656, 1000.000000000000227 ) ;
#90649=EDGE_CURVE ( 'NONE', #33187, #92519, #142540, .T. ) ;
#90651=EDGE_CURVE ( 'NONE', #68408, #100403, #31629, .T. ) ;
#90652=DIRECTION ( 'NONE',  ( 0.3543493200069163240, 0.000000000000000000, -0.9351131265310288487 ) ) ;
#90653=CARTESIAN_POINT ( 'NONE',  ( -0.7071067811865329178, -15.74070752338412760, 5.000000000000000000 ) ) ;
#90656=ADVANCED_FACE ( 'NONE', ( #76581 ), #75852, .F. ) ;
#90657=VECTOR ( 'NONE', #76765, 1000.000000000000000 ) ;
#90659=ORIENTED_EDGE ( 'NONE', *, *, #54320, .F. ) ;
#90661=ORIENTED_EDGE ( 'NONE', *, *, #41495, .T. ) ;
#90663=VECTOR ( 'NONE', #68008, 1000.000000000000000 ) ;
#90664=DIRECTION ( 'NONE',  ( 0.7071067811865486830, -0.7071067811865464625, -0.000000000000000000 ) ) ;
#90665=ADVANCED_FACE ( 'NONE', ( #7706 ), #120016, .F. ) ;
#90666=ORIENTED_EDGE ( 'NONE', *, *, #23051, .F. ) ;
#90667=ORIENTED_EDGE ( 'NONE', *, *, #50354, .T. ) ;
#90668=EDGE_LOOP ( 'NONE', ( #103152, #71930, #21132, #126526, #47871 ) ) ;
#90670=FACE_OUTER_BOUND ( 'NONE', #128007, .T. ) ;
#90672=EDGE_CURVE ( 'NONE', #89139, #47131, #21464, .T. ) ;
#90674=VERTEX_POINT ( 'NONE', #65728 ) ;
#90675=ORIENTED_EDGE ( 'NONE', *, *, #89035, .F. ) ;
#90676=CARTESIAN_POINT ( 'NONE',  ( -20.81601139373100295, 28.73617430169773002, 5.000000000000000000 ) ) ;
#90677=VERTEX_POINT ( 'NONE', #18566 ) ;
#90678=ORIENTED_EDGE ( 'NONE', *, *, #49602, .F. ) ;
#90679=VECTOR ( 'NONE', #99340, 1000.000000000000000 ) ;
#90680=ORIENTED_EDGE ( 'NONE', *, *, #4316, .F. ) ;
#90681=VECTOR ( 'NONE', #59582, 1000.000000000000227 ) ;
#90682=DIRECTION ( 'NONE',  ( -0.7071067811865487940, 0.7071067811865463515, -0.000000000000000000 ) ) ;
#90683=EDGE_CURVE ( 'NONE', #25059, #45102, #9098, .T. ) ;
#90684=CARTESIAN_POINT ( 'NONE',  ( -20.20710678118641113, 18.75929247661552779, 5.000000000000000000 ) ) ;
#90687=DIRECTION ( 'NONE',  ( 0.3543493200069162685, -0.000000000000000000, -0.9351131265310288487 ) ) ;
#90690=CARTESIAN_POINT ( 'NONE',  ( 33.29974487139158867, -27.71228299555229313, 4.000000000000000000 ) ) ;
#90691=EDGE_CURVE ( 'NONE', #67860, #9144, #97577, .T. ) ;
#90692=FACE_BOUND ( 'NONE', #36137, .T. ) ;
#90693=ORIENTED_EDGE ( 'NONE', *, *, #71162, .T. ) ;
#90694=CARTESIAN_POINT ( 'NONE',  ( 11.99999999999992895, -0.4125381241607481431, 4.000000000000000000 ) ) ;
#90696=CARTESIAN_POINT ( 'NONE',  ( -21.47512612785032715, 14.25929247661557753, 9.797011795316587168 ) ) ;
#90697=VERTEX_POINT ( 'NONE', #129489 ) ;
#90698=DIRECTION ( 'NONE',  ( 1.000000000000000000, 0.000000000000000000, 0.000000000000000000 ) ) ;
#90700=ORIENTED_EDGE ( 'NONE', *, *, #19434, .T. ) ;
#90701=VECTOR ( 'NONE', #110879, 999.9999999999998863 ) ;
#90702=ORIENTED_EDGE ( 'NONE', *, *, #13092, .F. ) ;
#90704=ORIENTED_EDGE ( 'NONE', *, *, #11344, .F. ) ;
#90707=EDGE_CURVE ( 'NONE', #10935, #126541, #124339, .T. ) ;
#90708=ORIENTED_EDGE ( 'NONE', *, *, #38123, .F. ) ;
#90710=FACE_OUTER_BOUND ( 'NONE', #30531, .T. ) ;
#90711=VECTOR ( 'NONE', #129418, 999.9999999999998863 ) ;
#90713=VECTOR ( 'NONE', #106356, 1000.000000000000114 ) ;
#90714=AXIS2_PLACEMENT_3D ( 'NONE', #79311, #24167, #113294 ) ;
#90717=CARTESIAN_POINT ( 'NONE',  ( 27.79333936457828358, 21.75929247661549226, 4.998822639870708073 ) ) ;
#90719=CARTESIAN_POINT ( 'NONE',  ( -17.29289321881334018, -15.74070752338413470, 5.000000000000000000 ) ) ;
#90720=VERTEX_POINT ( 'NONE', #68558 ) ;
#90723=AXIS2_PLACEMENT_3D ( 'NONE', #25882, #57826, #91170 ) ;
#90724=ORIENTED_EDGE ( 'NONE', *, *, #30900, .T. ) ;
#90726=EDGE_LOOP ( 'NONE', ( #90192, #70545, #129223, #8544, #138823 ) ) ;
#90727=CARTESIAN_POINT ( 'NONE',  ( -12.29974487139158512, -27.71228299555214747, 4.000000000000000000 ) ) ;
#90728=EDGE_LOOP ( 'NONE', ( #24312, #83548, #27089, #90860, #5059 ) ) ;
#90729=VECTOR ( 'NONE', #96394, 1000.000000000000000 ) ;
#90730=ORIENTED_EDGE ( 'NONE', *, *, #5989, .T. ) ;
#90732=ADVANCED_FACE ( 'NONE', ( #46835 ), #25006, .F. ) ;
#90733=PLANE ( 'NONE',  #136537 ) ;
#90734=ORIENTED_EDGE ( 'NONE', *, *, #39901, .F. ) ;
#90735=VECTOR ( 'NONE', #128452, 999.9999999999998863 ) ;
#90737=CARTESIAN_POINT ( 'NONE',  ( 39.29974487139159578, -27.71228299555233576, 4.000000000000000000 ) ) ;
#90740=DIRECTION ( 'NONE',  ( 0.7071067811865487940, 0.7071067811865463515, 0.000000000000000000 ) ) ;
#90741=ORIENTED_EDGE ( 'NONE', *, *, #77749, .T. ) ;
#90743=CARTESIAN_POINT ( 'NONE',  ( -30.29974487139158867, -27.71228299555227537, 4.000000000000000000 ) ) ;
#90744=LINE ( 'NONE', #12433, #74382 ) ;
#90745=CARTESIAN_POINT ( 'NONE',  ( -15.33010218547255832, 17.25929247661554555, 19.83885114516074921 ) ) ;
#90746=ORIENTED_EDGE ( 'NONE', *, *, #109343, .F. ) ;
#90747=PLANE ( 'NONE',  #102855 ) ;
#90748=DIRECTION ( 'NONE',  ( 0.7071067811865486830, -0.7071067811865464625, -0.000000000000000000 ) ) ;
#90749=ORIENTED_EDGE ( 'NONE', *, *, #116017, .F. ) ;
#90750=CARTESIAN_POINT ( 'NONE',  ( 31.49999999999977973, -10.91253812416064228, 4.000000000000000000 ) ) ;
#90751=ORIENTED_EDGE ( 'NONE', *, *, #101070, .F. ) ;
#90752=LINE ( 'NONE', #44404, #84643 ) ;
#90753=LINE ( 'NONE', #134983, #114076 ) ;
#90755=ORIENTED_EDGE ( 'NONE', *, *, #77483, .F. ) ;
#90756=EDGE_CURVE ( 'NONE', #138480, #118870, #79461, .T. ) ;
#90758=PLANE ( 'NONE',  #94517 ) ;
#90760=EDGE_CURVE ( 'NONE', #30354, #103699, #112745, .T. ) ;
#90762=FACE_OUTER_BOUND ( 'NONE', #140917, .T. ) ;
#90763=ORIENTED_EDGE ( 'NONE', *, *, #89283, .T. ) ;
#90764=VECTOR ( 'NONE', #56785, 1000.000000000000000 ) ;
#90765=CARTESIAN_POINT ( 'NONE',  ( 53.99451991528749062, 28.92564299267975869, 4.000000000000000000 ) ) ;
#90766=EDGE_LOOP ( 'NONE', ( #140878, #125427, #94192 ) ) ;
#90767=PLANE ( 'NONE',  #90140 ) ;
#90768=DIRECTION ( 'NONE',  ( -0.7071067811865486830, -0.7071067811865464625, 0.000000000000000000 ) ) ;
#90769=ORIENTED_EDGE ( 'NONE', *, *, #34001, .F. ) ;
#90770=EDGE_CURVE ( 'NONE', #39702, #35602, #13406, .T. ) ;
#90771=EDGE_LOOP ( 'NONE', ( #53354, #829, #124281, #64339 ) ) ;
#90773=LINE ( 'NONE', #92152, #113172 ) ;
#90774=VECTOR ( 'NONE', #67724, 1000.000000000000000 ) ;
#90775=VERTEX_POINT ( 'NONE', #43934 ) ;
#90776=LINE ( 'NONE', #24773, #101692 ) ;
#90778=CARTESIAN_POINT ( 'NONE',  ( 23.29289321881329400, 14.25929247661557753, 5.000000000000000000 ) ) ;
#90780=VECTOR ( 'NONE', #91879, 1000.000000000000000 ) ;
#90781=CARTESIAN_POINT ( 'NONE',  ( 63.48921356237309510, -27.52281430457099631, 5.000000000000000000 ) ) ;
#90782=DIRECTION ( 'NONE',  ( 0.7071067811865486830, -0.7071067811865464625, -0.000000000000000000 ) ) ;
#90783=AXIS2_PLACEMENT_3D ( 'NONE', #23156, #110875, #100047 ) ;
#90784=LINE ( 'NONE', #113937, #46073 ) ;
#90785=DIRECTION ( 'NONE',  ( -0.7071067811865486830, -0.7071067811865464625, 0.000000000000000000 ) ) ;
#90787=EDGE_LOOP ( 'NONE', ( #120619, #132920, #8097, #17621 ) ) ;
#90788=ORIENTED_EDGE ( 'NONE', *, *, #39218, .F. ) ;
#90790=ORIENTED_EDGE ( 'NONE', *, *, #96809, .T. ) ;
#90791=VERTEX_POINT ( 'NONE', #80152 ) ;
#90792=ORIENTED_EDGE ( 'NONE', *, *, #117004, .F. ) ;
#90793=AXIS2_PLACEMENT_3D ( 'NONE', #10995, #34950, #90004 ) ;
#90794=LINE ( 'NONE', #13893, #82623 ) ;
#90795=DIRECTION ( 'NONE',  ( 1.000000000000000000, 0.000000000000000000, 0.000000000000000000 ) ) ;
#90796=ORIENTED_EDGE ( 'NONE', *, *, #65268, .T. ) ;
#90797=CARTESIAN_POINT ( 'NONE',  ( 34.92499999999998295, -21.72500000000000142, 5.000000000000000000 ) ) ;
#90799=FACE_OUTER_BOUND ( 'NONE', #45234, .T. ) ;
#90800=CARTESIAN_POINT ( 'NONE',  ( 8.999999999999937828, 13.93112307739204425, 4.000000000000000000 ) ) ;
#90802=VERTEX_POINT ( 'NONE', #2528 ) ;
#90803=PLANE ( 'NONE',  #113595 ) ;
#90805=DIRECTION ( 'NONE',  ( 0.6830127018922180770, -0.6830127018922204085, -0.2588190451025213501 ) ) ;
#90808=DIRECTION ( 'NONE',  ( 0.7071067811865487940, 0.7071067811865463515, 0.000000000000000000 ) ) ;
#90809=CARTESIAN_POINT ( 'NONE',  ( 2.816011393730999401, 28.73617430169785436, 5.000000000000000000 ) ) ;
#90811=LINE ( 'NONE', #21955, #374 ) ;
#90813=DIRECTION ( 'NONE',  ( 1.000000000000000000, 0.000000000000000000, 0.000000000000000000 ) ) ;
#90814=ORIENTED_EDGE ( 'NONE', *, *, #81494, .F. ) ;
#90815=ORIENTED_EDGE ( 'NONE', *, *, #60258, .F. ) ;
#90817=EDGE_CURVE ( 'NONE', #64329, #137485, #22845, .T. ) ;
#90818=ORIENTED_EDGE ( 'NONE', *, *, #79584, .F. ) ;
#90819=CARTESIAN_POINT ( 'NONE',  ( -34.47516574401891631, -10.50948238788427425, 4.998110765256835286 ) ) ;
#90822=AXIS2_PLACEMENT_3D ( 'NONE', #87894, #21209, #111042 ) ;
#90823=VECTOR ( 'NONE', #64895, 999.9999999999998863 ) ;
#90824=VECTOR ( 'NONE', #125428, 1000.000000000000000 ) ;
#90825=EDGE_CURVE ( 'NONE', #102617, #105152, #14132, .T. ) ;
#90826=LINE ( 'NONE', #37874, #112771 ) ;
#90827=PLANE ( 'NONE',  #120908 ) ;
#90828=VECTOR ( 'NONE', #65625, 1000.000000000000000 ) ;
#90829=VECTOR ( 'NONE', #26138, 1000.000000000000000 ) ;
#90832=EDGE_CURVE ( 'NONE', #29747, #61512, #67113, .T. ) ;
#90834=ORIENTED_EDGE ( 'NONE', *, *, #52177, .T. ) ;
#90839=CARTESIAN_POINT ( 'NONE',  ( 3.183988606268992161, 28.73617430169789699, 5.000000000000000000 ) ) ;
#90840=DIRECTION ( 'NONE',  ( -0.7071067811865486830, -0.7071067811865464625, -0.000000000000000000 ) ) ;
#90841=ADVANCED_FACE ( 'NONE', ( #99721 ), #58424, .F. ) ;
#90843=ORIENTED_EDGE ( 'NONE', *, *, #121642, .T. ) ;
#90846=VERTEX_POINT ( 'NONE', #122915 ) ;
#90847=CARTESIAN_POINT ( 'NONE',  ( 34.42499999999998295, 22.22500000000000142, 5.000000000000000000 ) ) ;
#90848=DIRECTION ( 'NONE',  ( -0.000000000000000000, -0.3543493200069152693, 0.9351131265310292928 ) ) ;
#90849=DIRECTION ( 'NONE',  ( -0.6830127018922181881, 0.6830127018922202975, -0.2588190451025214056 ) ) ;
#90850=DIRECTION ( 'NONE',  ( -0.7071067811865486830, -0.7071067811865464625, -0.000000000000000000 ) ) ;
#90851=EDGE_CURVE ( 'NONE', #9933, #99443, #33092, .T. ) ;
#90854=CARTESIAN_POINT ( 'NONE',  ( 17.99999999999987921, 20.96639925780205260, 5.000000000000000000 ) ) ;
#90855=DIRECTION ( 'NONE',  ( -0.7071067811865486830, -0.7071067811865464625, 0.000000000000000000 ) ) ;
#90856=CARTESIAN_POINT ( 'NONE',  ( -31.49999999999977973, 19.46639925780206326, 5.000000000000000000 ) ) ;
#90857=EDGE_LOOP ( 'NONE', ( #111506, #114865, #45654, #52556 ) ) ;
#90860=ORIENTED_EDGE ( 'NONE', *, *, #124051, .T. ) ;
#90861=VECTOR ( 'NONE', #60226, 1000.000000000000114 ) ;
#90862=PLANE ( 'NONE',  #65080 ) ;
#90863=VERTEX_POINT ( 'NONE', #77305 ) ;
#90865=DIRECTION ( 'NONE',  ( -0.000000000000000000, 0.000000000000000000, 1.000000000000000000 ) ) ;
#90866=EDGE_CURVE ( 'NONE', #123433, #98806, #88881, .T. ) ;
#90867=LINE ( 'NONE', #47393, #8474 ) ;
#90869=CARTESIAN_POINT ( 'NONE',  ( -19.05000000000000071, 3.174999999999997158, 1.444000000000000394 ) ) ;
#90870=FACE_BOUND ( 'NONE', #116393, .T. ) ;
#90871=CARTESIAN_POINT ( 'NONE',  ( 0.4892135623730947680, -27.52281430457055578, 5.000000000000000000 ) ) ;
#90872=FACE_OUTER_BOUND ( 'NONE', #68917, .T. ) ;
#90873=LINE ( 'NONE', #45241, #45685 ) ;
#90875=CARTESIAN_POINT ( 'NONE',  ( 75.48921356237309510, -27.52281430457107803, 5.000000000000000000 ) ) ;
#90877=ORIENTED_EDGE ( 'NONE', *, *, #87175, .F. ) ;
#90878=LINE ( 'NONE', #48790, #141250 ) ;
#90880=ADVANCED_FACE ( 'NONE', ( #1793 ), #90269, .F. ) ;
#90881=ORIENTED_EDGE ( 'NONE', *, *, #126807, .F. ) ;
#90882=ORIENTED_EDGE ( 'NONE', *, *, #44385, .T. ) ;
#90885=FACE_OUTER_BOUND ( 'NONE', #28129, .T. ) ;
#90886=ADVANCED_FACE ( 'NONE', ( #39488 ), #37339, .T. ) ;
#90887=VECTOR ( 'NONE', #133115, 1000.000000000000000 ) ;
#90888=EDGE_LOOP ( 'NONE', ( #115880, #22640, #49873, #138383 ) ) ;
#90889=CARTESIAN_POINT ( 'NONE',  ( 0.000000000000000000, -11.35517001088072142, -1.126524801160109890 ) ) ;
#90892=CARTESIAN_POINT ( 'NONE',  ( 3.758600742197928835, 21.72499999999999432, 5.000000000000000000 ) ) ;
#90893=EDGE_CURVE ( 'NONE', #57216, #76385, #59130, .T. ) ;
#90896=PLANE ( 'NONE',  #109416 ) ;
#90898=ORIENTED_EDGE ( 'NONE', *, *, #71779, .T. ) ;
#90900=LINE ( 'NONE', #32963, #86693 ) ;
#90901=CARTESIAN_POINT ( 'NONE',  ( 20.27718569542926730, -21.72500000000000853, 5.000000000000000000 ) ) ;
#90902=EDGE_LOOP ( 'NONE', ( #68235, #1699, #129259, #51144 ) ) ;
#90903=VERTEX_POINT ( 'NONE', #26456 ) ;
#90904=ORIENTED_EDGE ( 'NONE', *, *, #36182, .T. ) ;
#90905=EDGE_CURVE ( 'NONE', #137076, #142844, #3254, .T. ) ;
#90907=AXIS2_PLACEMENT_3D ( 'NONE', #130573, #11592, #55876 ) ;
#90908=ORIENTED_EDGE ( 'NONE', *, *, #134238, .F. ) ;
#90909=DIRECTION ( 'NONE',  ( -0.6830127018922180770, -0.6830127018922204085, -0.2588190451025213501 ) ) ;
#90910=DIRECTION ( 'NONE',  ( 0.7071067811865487940, 0.7071067811865463515, 0.000000000000000000 ) ) ;
#90912=CARTESIAN_POINT ( 'NONE',  ( 9.792893218813393474, -5.240707523384230626, 5.000000000000000000 ) ) ;
#90913=ORIENTED_EDGE ( 'NONE', *, *, #92850, .T. ) ;
#90914=CARTESIAN_POINT ( 'NONE',  ( -45.48921356237309510, -27.52281430457087197, 5.000000000000000000 ) ) ;
#90915=CARTESIAN_POINT ( 'NONE',  ( -17.99999999999986855, -18.03360074219755660, 5.000000000000000000 ) ) ;
#90916=DIRECTION ( 'NONE',  ( -0.7071067811865487940, 0.7071067811865463515, 0.000000000000000000 ) ) ;
#90917=VECTOR ( 'NONE', #31370, 1000.000000000000000 ) ;
#90919=ORIENTED_EDGE ( 'NONE', *, *, #48558, .F. ) ;
#90920=VECTOR ( 'NONE', #101709, 1000.000000000000227 ) ;
#90921=ORIENTED_EDGE ( 'NONE', *, *, #45482, .F. ) ;
#90922=DIRECTION ( 'NONE',  ( -0.7071067811865486830, -0.7071067811865464625, -0.000000000000000000 ) ) ;
#90923=CARTESIAN_POINT ( 'NONE',  ( 30.32816939922332367, -3.740707523384241728, 4.000000000000000000 ) ) ;
#90925=CARTESIAN_POINT ( 'NONE',  ( -7.433128002487371155, -21.74070752338405654, 6.915939825044092437 ) ) ;
#90926=VECTOR ( 'NONE', #128506, 999.9999999999998863 ) ;
#90927=ORIENTED_EDGE ( 'NONE', *, *, #102486, .T. ) ;
#90928=DIRECTION ( 'NONE',  ( 1.000000000000000000, 0.000000000000000000, 0.000000000000000000 ) ) ;
#90929=FACE_OUTER_BOUND ( 'NONE', #50255, .T. ) ;
#90930=EDGE_CURVE ( 'NONE', #130856, #16952, #5385, .T. ) ;
#90931=CARTESIAN_POINT ( 'NONE',  ( 34.92499999999998295, 11.81665438641033106, 4.500000000000000888 ) ) ;
#90932=DIRECTION ( 'NONE',  ( 0.3543493200069163240, -0.000000000000000000, -0.9351131265310288487 ) ) ;
#90933=DIRECTION ( 'NONE',  ( 0.6830127018922180770, -0.6830127018922204085, -0.2588190451025213501 ) ) ;
#90934=VECTOR ( 'NONE', #87942, 999.9999999999998863 ) ;
#90935=VECTOR ( 'NONE', #83132, 1000.000000000000227 ) ;
#90936=DIRECTION ( 'NONE',  ( 0.7071067811865486830, -0.7071067811865464625, -0.000000000000000000 ) ) ;
#90937=CARTESIAN_POINT ( 'NONE',  ( 13.37176554955607166, -8.240707523384193323, 11.38925528200749682 ) ) ;
#90940=EDGE_CURVE ( 'NONE', #132371, #136694, #15530, .T. ) ;
#90941=CARTESIAN_POINT ( 'NONE',  ( 30.29974487139158867, -27.71228299555227537, 4.000000000000000000 ) ) ;
#90942=ORIENTED_EDGE ( 'NONE', *, *, #2924, .T. ) ;
#90944=ORIENTED_EDGE ( 'NONE', *, *, #61549, .F. ) ;
#90945=CARTESIAN_POINT ( 'NONE',  ( 28.49999999999980460, -13.53360074219760101, 5.000000000000000000 ) ) ;
#90947=DIRECTION ( 'NONE',  ( 0.3543493200069162685, -0.000000000000000000, -0.9351131265310288487 ) ) ;
#90948=AXIS2_PLACEMENT_3D ( 'NONE', #59753, #72078, #116250 ) ;
#90949=CARTESIAN_POINT ( 'NONE',  ( -2.671830600776455178, -12.74070752338415602, 4.000000000000000000 ) ) ;
#90950=CARTESIAN_POINT ( 'NONE',  ( -25.49999999999981526, 7.087461875839175640, 4.000000000000000000 ) ) ;
#90951=CARTESIAN_POINT ( 'NONE',  ( 24.99507522778790758, -5.240707523384225297, 12.38332538355490442 ) ) ;
#90952=ORIENTED_EDGE ( 'NONE', *, *, #76985, .T. ) ;
#90953=LINE ( 'NONE', #1730, #14050 ) ;
#90954=CARTESIAN_POINT ( 'NONE',  ( -13.49999999999990408, -10.04351517176479014, -1.623559851933856102 ) ) ;
#90955=LINE ( 'NONE', #2464, #136199 ) ;
#90957=ADVANCED_FACE ( 'NONE', ( #48936 ), #138072, .T. ) ;
#90958=AXIS2_PLACEMENT_3D ( 'NONE', #57214, #125296, #47772 ) ;
#90959=CARTESIAN_POINT ( 'NONE',  ( -20.81601139373100295, 28.73617430169773002, 5.000000000000000000 ) ) ;
#90960=CARTESIAN_POINT ( 'NONE',  ( 5.671830600776431197, -3.740707523384244837, 4.000000000000000000 ) ) ;
#90961=LINE ( 'NONE', #98002, #83465 ) ;
#90965=ORIENTED_EDGE ( 'NONE', *, *, #34340, .F. ) ;
#90966=AXIS2_PLACEMENT_3D ( 'NONE', #5370, #18372, #82964 ) ;
#90969=CARTESIAN_POINT ( 'NONE',  ( -75.18398860626899705, 28.73617430169839793, 5.000000000000000000 ) ) ;
#90970=CARTESIAN_POINT ( 'NONE',  ( -14.67183060077636725, 17.25929247661554200, 4.000000000000000000 ) ) ;
#90971=CARTESIAN_POINT ( 'NONE',  ( -26.51078643762690845, -27.52281430457036748, 5.000000000000000000 ) ) ;
#90973=DIRECTION ( 'NONE',  ( -0.7071067811865487940, 0.7071067811865463515, -0.000000000000000000 ) ) ;
#90974=ORIENTED_EDGE ( 'NONE', *, *, #141269, .T. ) ;
#90975=ORIENTED_EDGE ( 'NONE', *, *, #85187, .F. ) ;
#90976=CARTESIAN_POINT ( 'NONE',  ( 30.29974487139158867, -27.71228299555227537, 4.000000000000000000 ) ) ;
#90977=PLANE ( 'NONE',  #67778 ) ;
#90979=CARTESIAN_POINT ( 'NONE',  ( -69.18398860626899705, 28.73617430169835529, 5.000000000000000000 ) ) ;
#90980=DIRECTION ( 'NONE',  ( 0.7071067811865486830, -0.7071067811865464625, -0.000000000000000000 ) ) ;
#90982=EDGE_CURVE ( 'NONE', #62013, #135631, #137369, .T. ) ;
#90984=PLANE ( 'NONE',  #37003 ) ;
#90985=ADVANCED_FACE ( 'NONE', ( #91702 ), #126458, .T. ) ;
#90987=VERTEX_POINT ( 'NONE', #6080 ) ;
#90989=CARTESIAN_POINT ( 'NONE',  ( 54.18398860626899705, 28.73617430169825226, 5.000000000000000000 ) ) ;
#90990=EDGE_CURVE ( 'NONE', #12370, #130351, #60546, .T. ) ;
#90991=CARTESIAN_POINT ( 'NONE',  ( -33.29974487139158867, -27.71228299555229313, 4.000000000000000000 ) ) ;
#90992=LINE ( 'NONE', #35908, #123875 ) ;
#90993=VECTOR ( 'NONE', #70557, 1000.000000000000000 ) ;
#90994=VECTOR ( 'NONE', #96278, 1000.000000000000227 ) ;
#90995=ORIENTED_EDGE ( 'NONE', *, *, #115451, .T. ) ;
#90996=ADVANCED_FACE ( 'NONE', ( #105423 ), #127179, .F. ) ;
#90998=LINE ( 'NONE', #14829, #5076 ) ;
#90999=PLANE ( 'NONE',  #51368 ) ;
#91001=DIRECTION ( 'NONE',  ( -0.7071067811865486830, -0.7071067811865464625, 0.000000000000000000 ) ) ;
#91002=VERTEX_POINT ( 'NONE', #98143 ) ;
#91003=ORIENTED_EDGE ( 'NONE', *, *, #33946, .T. ) ;
#91004=VECTOR ( 'NONE', #112235, 1000.000000000000000 ) ;
#91006=LINE ( 'NONE', #80138, #41993 ) ;
#91007=EDGE_CURVE ( 'NONE', #54885, #15309, #142367, .T. ) ;
#91009=EDGE_CURVE ( 'NONE', #91146, #94083, #118442, .T. ) ;
#91010=CARTESIAN_POINT ( 'NONE',  ( 26.99999999999981881, 17.58746187583906107, 4.000000000000000000 ) ) ;
#91011=DIRECTION ( 'NONE',  ( -0.7071067811865487940, 0.7071067811865463515, -0.000000000000000000 ) ) ;
#91013=PLANE ( 'NONE',  #50707 ) ;
#91014=DIRECTION ( 'NONE',  ( 0.6830127018922180770, -0.6830127018922204085, -0.2588190451025213501 ) ) ;
#91015=AXIS2_PLACEMENT_3D ( 'NONE', #34646, #2706, #12859 ) ;
#91016=LINE ( 'NONE', #91696, #37817 ) ;
#91018=VERTEX_POINT ( 'NONE', #8230 ) ;
#91019=ADVANCED_FACE ( 'NONE', ( #52473 ), #130792, .T. ) ;
#91020=ORIENTED_EDGE ( 'NONE', *, *, #130962, .T. ) ;
#91022=ORIENTED_EDGE ( 'NONE', *, *, #109184, .F. ) ;
#91023=DIRECTION ( 'NONE',  ( -0.7071067811865486830, -0.7071067811865464625, 0.000000000000000000 ) ) ;
#91024=CARTESIAN_POINT ( 'NONE',  ( -3.299744871391591339, -27.71228299555208352, 4.000000000000000000 ) ) ;
#91025=CYLINDRICAL_SURFACE ( 'NONE', #128956, 0.5000000000000004441 ) ;
#91026=DIRECTION ( 'NONE',  ( 1.000000000000000000, 0.000000000000000000, 0.000000000000000000 ) ) ;
#91027=CARTESIAN_POINT ( 'NONE',  ( 24.18398860626899705, 28.73617430169804265, 5.000000000000000000 ) ) ;
#91028=ORIENTED_EDGE ( 'NONE', *, *, #102266, .F. ) ;
#91030=ADVANCED_FACE ( 'NONE', ( #64080 ), #32162, .F. ) ;
#91031=AXIS2_PLACEMENT_3D ( 'NONE', #40491, #93422, #52064 ) ;
#91032=CARTESIAN_POINT ( 'NONE',  ( 28.17183060077626777, -8.240707523384203981, 4.000000000000000000 ) ) ;
#91034=AXIS2_PLACEMENT_3D ( 'NONE', #121203, #111023, #77030 ) ;
#91035=VECTOR ( 'NONE', #69138, 1000.000000000000000 ) ;
#91036=EDGE_LOOP ( 'NONE', ( #38468, #83417, #28247, #38238 ) ) ;
#91039=LINE ( 'NONE', #77320, #129008 ) ;
#91040=ADVANCED_FACE ( 'NONE', ( #75678 ), #117702, .T. ) ;
#91041=DIRECTION ( 'NONE',  ( -0.7071067811865486830, -0.7071067811865464625, 0.000000000000000000 ) ) ;
#91042=AXIS2_PLACEMENT_3D ( 'NONE', #92958, #15360, #83535 ) ;
#91043=ORIENTED_EDGE ( 'NONE', *, *, #48182, .T. ) ;
#91044=FACE_BOUND ( 'NONE', #107242, .T. ) ;
#91045=DIRECTION ( 'NONE',  ( -0.7071067811865487940, 0.7071067811865463515, -0.000000000000000000 ) ) ;
#91046=ADVANCED_FACE ( 'NONE', ( #140905 ), #40902, .T. ) ;
#91047=FACE_OUTER_BOUND ( 'NONE', #119709, .T. ) ;
#91050=LINE ( 'NONE', #79488, #67504 ) ;
#91053=EDGE_LOOP ( 'NONE', ( #111573, #80318, #13182, #1604 ) ) ;
#91054=VECTOR ( 'NONE', #100216, 1000.000000000000000 ) ;
#91057=ORIENTED_EDGE ( 'NONE', *, *, #122710, .F. ) ;
#91058=CARTESIAN_POINT ( 'NONE',  ( -7.773258392821613683, -11.24070752338416135, 18.24660765846980937 ) ) ;
#91059=ORIENTED_EDGE ( 'NONE', *, *, #26051, .F. ) ;
#91060=CARTESIAN_POINT ( 'NONE',  ( -34.92500000000001137, -21.72500000000000142, 4.500000000000000888 ) ) ;
#91061=DIRECTION ( 'NONE',  ( -0.000000000000000000, -1.000000000000000000, -0.000000000000000000 ) ) ;
#91062=LINE ( 'NONE', #69296, #44856 ) ;
#91063=ORIENTED_EDGE ( 'NONE', *, *, #114816, .F. ) ;
#91069=CARTESIAN_POINT ( 'NONE',  ( -14.99999999999989875, 2.342191155542430181, -5.001666872980051970 ) ) ;
#91070=LINE ( 'NONE', #78751, #106963 ) ;
#91071=ORIENTED_EDGE ( 'NONE', *, *, #93219, .T. ) ;
#91072=DIRECTION ( 'NONE',  ( -0.7071067811865486830, -0.7071067811865464625, 0.000000000000000000 ) ) ;
#91073=CARTESIAN_POINT ( 'NONE',  ( 0.000000000000000000, 0.000000000000000000, 5.000000000000000000 ) ) ;
#91074=VECTOR ( 'NONE', #44602, 1000.000000000000000 ) ;
#91075=ORIENTED_EDGE ( 'NONE', *, *, #28274, .F. ) ;
#91076=VERTEX_POINT ( 'NONE', #11085 ) ;
#91077=EDGE_CURVE ( 'NONE', #96885, #63562, #135084, .T. ) ;
#91078=ORIENTED_EDGE ( 'NONE', *, *, #28799, .T. ) ;
#91080=ORIENTED_EDGE ( 'NONE', *, *, #5050, .T. ) ;
#91081=VECTOR ( 'NONE', #46880, 1000.000000000000000 ) ;
#91085=CARTESIAN_POINT ( 'NONE',  ( -34.45011844616454511, 19.51628081163728723, 5.000000000000000888 ) ) ;
#91086=ORIENTED_EDGE ( 'NONE', *, *, #22940, .T. ) ;
#91087=CARTESIAN_POINT ( 'NONE',  ( 34.92499999999998295, 9.691175483026997384, 9.749534648445568052 ) ) ;
#91088=ORIENTED_EDGE ( 'NONE', *, *, #92771, .F. ) ;
#91090=VECTOR ( 'NONE', #57844, 1000.000000000000000 ) ;
#91091=PLANE ( 'NONE',  #121132 ) ;
#91092=ORIENTED_EDGE ( 'NONE', *, *, #125911, .F. ) ;
#91093=( BOUNDED_CURVE ( )  B_SPLINE_CURVE ( 3, ( #7055, #71659, #4911, #73103 ),
 .UNSPECIFIED., .F., .F. ) 
 B_SPLINE_CURVE_WITH_KNOTS ( ( 4, 4 ),
 ( 2.001653308786169649, 3.503810798801449522 ),
 .UNSPECIFIED. ) 
 CURVE ( )  GEOMETRIC_REPRESENTATION_ITEM ( )  RATIONAL_B_SPLINE_CURVE ( ( 1.000000000000000000, 0.8206354192515243895, 0.8206354192515243895, 1.000000000000000000 ) ) 
 REPRESENTATION_ITEM ( '' )  );
#91094=LINE ( 'NONE', #122245, #28302 ) ;
#91095=DIRECTION ( 'NONE',  ( -0.000000000000000000, 0.3543493200069153248, 0.9351131265310292928 ) ) ;
#91097=ORIENTED_EDGE ( 'NONE', *, *, #35784, .F. ) ;
#91099=EDGE_CURVE ( 'NONE', #2653, #98498, #21290, .T. ) ;
#91100=ORIENTED_EDGE ( 'NONE', *, *, #60228, .T. ) ;
#91101=ORIENTED_EDGE ( 'NONE', *, *, #52016, .F. ) ;
#91103=LINE ( 'NONE', #45464, #91104 ) ;
#91104=VECTOR ( 'NONE', #133871, 1000.000000000000227 ) ;
#91105=LINE ( 'NONE', #16337, #111742 ) ;
#91110=DIRECTION ( 'NONE',  ( 0.7071067811865487940, -0.7071067811865463515, 0.000000000000000000 ) ) ;
#91112=ORIENTED_EDGE ( 'NONE', *, *, #97878, .F. ) ;
#91115=LINE ( 'NONE', #78085, #97074 ) ;
#91116=VECTOR ( 'NONE', #94070, 1000.000000000000227 ) ;
#91117=CARTESIAN_POINT ( 'NONE',  ( 28.04515773336648721, -21.74070752338406365, 21.72585301388591361 ) ) ;
#91118=EDGE_CURVE ( 'NONE', #123251, #53550, #45916, .T. ) ;
#91120=ORIENTED_EDGE ( 'NONE', *, *, #7377, .F. ) ;
#91122=EDGE_LOOP ( 'NONE', ( #52061, #93149, #132666 ) ) ;
#91124=DIRECTION ( 'NONE',  ( 0.6830127018922180770, -0.6830127018922204085, -0.2588190451025213501 ) ) ;
#91126=DIRECTION ( 'NONE',  ( 1.000000000000000000, 0.000000000000000000, 0.000000000000000000 ) ) ;
#91127=CARTESIAN_POINT ( 'NONE',  ( 34.45011844616451668, -11.99769585840593322, 5.000000000000000000 ) ) ;
#91128=FACE_OUTER_BOUND ( 'NONE', #20607, .T. ) ;
#91129=EDGE_CURVE ( 'NONE', #83991, #9245, #33619, .T. ) ;
#91131=LINE ( 'NONE', #1897, #48421 ) ;
#91132=CARTESIAN_POINT ( 'NONE',  ( 34.49999999999975842, 16.46425560840032531, 4.994342998332160555 ) ) ;
#91133=CARTESIAN_POINT ( 'NONE',  ( 32.99451991528749062, 28.92564299267960948, 4.000000000000000000 ) ) ;
#91135=DIRECTION ( 'NONE',  ( -0.7071067811865486830, -0.7071067811865464625, 0.000000000000000000 ) ) ;
#91136=DIRECTION ( 'NONE',  ( 0.7071067811865487940, 0.7071067811865463515, 0.000000000000000000 ) ) ;
#91137=VERTEX_POINT ( 'NONE', #90100 ) ;
#91138=EDGE_CURVE ( 'NONE', #10476, #91002, #109719, .T. ) ;
#91139=DIRECTION ( 'NONE',  ( -0.3543493200069163240, 0.000000000000000000, -0.9351131265310288487 ) ) ;
#91140=ORIENTED_EDGE ( 'NONE', *, *, #9729, .T. ) ;
#91141=FACE_OUTER_BOUND ( 'NONE', #59551, .T. ) ;
#91142=LINE ( 'NONE', #103391, #101986 ) ;
#91143=ORIENTED_EDGE ( 'NONE', *, *, #66779, .T. ) ;
#91144=LINE ( 'NONE', #79585, #118065 ) ;
#91145=LINE ( 'NONE', #123769, #125953 ) ;
#91146=VERTEX_POINT ( 'NONE', #32909 ) ;
#91147=CARTESIAN_POINT ( 'NONE',  ( -44.99451991528749772, 28.92564299267969474, 4.000000000000000000 ) ) ;
#91148=ORIENTED_EDGE ( 'NONE', *, *, #135363, .T. ) ;
#91149=CARTESIAN_POINT ( 'NONE',  ( -24.48921356237309510, -27.52281430457072631, 5.000000000000000000 ) ) ;
#91151=ORIENTED_EDGE ( 'NONE', *, *, #30777, .F. ) ;
#91152=DIRECTION ( 'NONE',  ( -0.000000000000000000, 0.3543493200069153248, 0.9351131265310292928 ) ) ;
#91154=PLANE ( 'NONE',  #83275 ) ;
#91155=CIRCLE ( 'NONE', #74913, 5.968999999999998529 ) ;
#91156=LINE ( 'NONE', #135377, #2226 ) ;
#91157=EDGE_LOOP ( 'NONE', ( #97242, #82236, #46317, #114293 ) ) ;
#91158=FACE_OUTER_BOUND ( 'NONE', #107061, .T. ) ;
#91159=DIRECTION ( 'NONE',  ( 0.6830127018922181881, 0.6830127018922202975, -0.2588190451025214056 ) ) ;
#91160=ADVANCED_FACE ( 'NONE', ( #77130 ), #23412, .F. ) ;
#91161=LINE ( 'NONE', #46973, #76283 ) ;
#91163=LINE ( 'NONE', #112881, #70025 ) ;
#91164=CARTESIAN_POINT ( 'NONE',  ( 39.18398860626899705, 28.73617430169814568, 5.000000000000000000 ) ) ;
#91165=CARTESIAN_POINT ( 'NONE',  ( -7.228506771386599361, 20.25929247661551003, 7.808871592221752422 ) ) ;
#91166=EDGE_LOOP ( 'NONE', ( #6329, #5724, #67719, #137747 ) ) ;
#91167=VECTOR ( 'NONE', #78597, 1000.000000000000227 ) ;
#91168=EDGE_CURVE ( 'NONE', #80483, #57964, #66939, .T. ) ;
#91169=EDGE_CURVE ( 'NONE', #136490, #64361, #21985, .T. ) ;
#91170=DIRECTION ( 'NONE',  ( 0.7071067811865487940, -0.7071067811865463515, 0.000000000000000000 ) ) ;
#91171=ORIENTED_EDGE ( 'NONE', *, *, #127176, .T. ) ;
#91174=DIRECTION ( 'NONE',  ( 1.000000000000000000, 0.000000000000000000, 0.000000000000000000 ) ) ;
#91175=DIRECTION ( 'NONE',  ( 0.000000000000000000, 0.000000000000000000, 1.000000000000000000 ) ) ;
#91176=DIRECTION ( 'NONE',  ( 1.000000000000000000, 0.000000000000000000, 0.000000000000000000 ) ) ;
#91177=DIRECTION ( 'NONE',  ( -0.7071067811865486830, -0.7071067811865464625, 0.000000000000000000 ) ) ;
#91178=ORIENTED_EDGE ( 'NONE', *, *, #5857, .T. ) ;
#91179=EDGE_CURVE ( 'NONE', #142746, #62063, #10389, .T. ) ;
#91181=VECTOR ( 'NONE', #48141, 1000.000000000000000 ) ;
#91182=LINE ( 'NONE', #89718, #139172 ) ;
#91183=EDGE_CURVE ( 'NONE', #88472, #12703, #56095, .T. ) ;
#91184=ORIENTED_EDGE ( 'NONE', *, *, #28185, .T. ) ;
#91185=PLANE ( 'NONE',  #120291 ) ;
#91186=EDGE_CURVE ( 'NONE', #71167, #98841, #24145, .T. ) ;
#91188=CARTESIAN_POINT ( 'NONE',  ( 27.29974487139158512, -27.71228299555225405, 4.000000000000000000 ) ) ;
#91189=ORIENTED_EDGE ( 'NONE', *, *, #38338, .T. ) ;
#91191=DIRECTION ( 'NONE',  ( -0.7071067811865487940, 0.7071067811865463515, -0.000000000000000000 ) ) ;
#91192=PLANE ( 'NONE',  #19167 ) ;
#91194=VECTOR ( 'NONE', #24416, 1000.000000000000000 ) ;
#91196=VECTOR ( 'NONE', #44548, 1000.000000000000000 ) ;
#91197=ORIENTED_EDGE ( 'NONE', *, *, #105664, .T. ) ;
#91198=ORIENTED_EDGE ( 'NONE', *, *, #18258, .T. ) ;
#91201=ADVANCED_FACE ( 'NONE', ( #133629 ), #34306, .T. ) ;
#91202=VECTOR ( 'NONE', #121708, 1000.000000000000000 ) ;
#91203=VERTEX_POINT ( 'NONE', #68400 ) ;
#91205=DIRECTION ( 'NONE',  ( 0.7071067811865486830, -0.7071067811865464625, -0.000000000000000000 ) ) ;
#91206=CARTESIAN_POINT ( 'NONE',  ( 13.49999999999991296, 0.05218569542916363935, 5.000000000000000000 ) ) ;
#91207=VECTOR ( 'NONE', #35342, 1000.000000000000000 ) ;
#91208=DIRECTION ( 'NONE',  ( 0.7071067811865486830, -0.7071067811865464625, -0.000000000000000000 ) ) ;
#91209=PLANE ( 'NONE',  #31851 ) ;
#91211=ADVANCED_FACE ( 'NONE', ( #83347 ), #115936, .F. ) ;
#91213=CARTESIAN_POINT ( 'NONE',  ( 4.499999999999968914, -10.04351517176477948, -1.623559851933813469 ) ) ;
#91215=EDGE_LOOP ( 'NONE', ( #30617, #34097, #61520, #19850 ) ) ;
#91216=DIRECTION ( 'NONE',  ( -0.7071067811865486830, -0.7071067811865464625, 0.000000000000000000 ) ) ;
#91217=VECTOR ( 'NONE', #5993, 1000.000000000000000 ) ;
#91218=EDGE_CURVE ( 'NONE', #89614, #95146, #105083, .T. ) ;
#91219=CARTESIAN_POINT ( 'NONE',  ( -6.183988606268994381, 28.73617430169791476, 5.000000000000000000 ) ) ;
#91220=EDGE_LOOP ( 'NONE', ( #48086, #107345, #14241, #136692 ) ) ;
#91221=ORIENTED_EDGE ( 'NONE', *, *, #111807, .T. ) ;
#91222=FACE_OUTER_BOUND ( 'NONE', #58438, .T. ) ;
#91224=FACE_OUTER_BOUND ( 'NONE', #115437, .T. ) ;
#91226=DIRECTION ( 'NONE',  ( -0.7071067811865486830, -0.7071067811865464625, 0.000000000000000000 ) ) ;
#91229=EDGE_CURVE ( 'NONE', #83610, #131121, #24850, .T. ) ;
#91231=ORIENTED_EDGE ( 'NONE', *, *, #86027, .T. ) ;
#91233=PLANE ( 'NONE',  #13297 ) ;
#91234=ORIENTED_EDGE ( 'NONE', *, *, #71448, .T. ) ;
#91236=EDGE_CURVE ( 'NONE', #71568, #43634, #29649, .T. ) ;
#91238=DIRECTION ( 'NONE',  ( -0.000000000000000000, 0.000000000000000000, 1.000000000000000000 ) ) ;
#91239=ORIENTED_EDGE ( 'NONE', *, *, #23839, .T. ) ;
#91241=CARTESIAN_POINT ( 'NONE',  ( -3.989119713460488104, -22.02621442084247860, 4.990779571109225543 ) ) ;
#91243=DIRECTION ( 'NONE',  ( -0.6830127018922181881, 0.6830127018922202975, -0.2588190451025214056 ) ) ;
#91244=ORIENTED_EDGE ( 'NONE', *, *, #6850, .T. ) ;
#91245=DIRECTION ( 'NONE',  ( -0.000000000000000000, 0.3543493200069153248, 0.9351131265310292928 ) ) ;
#91247=EDGE_LOOP ( 'NONE', ( #109982, #56420, #113214, #137922 ) ) ;
#91248=CARTESIAN_POINT ( 'NONE',  ( -57.48921356237308800, -27.52281430457095368, 5.000000000000000000 ) ) ;
#91249=EDGE_LOOP ( 'NONE', ( #4281, #88349, #55940, #8282 ) ) ;
#91250=VERTEX_POINT ( 'NONE', #39866 ) ;
#91251=LINE ( 'NONE', #57201, #13491 ) ;
#91252=VERTEX_POINT ( 'NONE', #7892 ) ;
#91253=VERTEX_POINT ( 'NONE', #52134 ) ;
#91254=VECTOR ( 'NONE', #62722, 1000.000000000000000 ) ;
#91255=ORIENTED_EDGE ( 'NONE', *, *, #55911, .F. ) ;
#91256=CARTESIAN_POINT ( 'NONE',  ( -12.48921356237309155, -27.52281430457064104, 5.000000000000000000 ) ) ;
#91257=AXIS2_PLACEMENT_3D ( 'NONE', #102009, #91159, #68004 ) ;
#91261=CARTESIAN_POINT ( 'NONE',  ( -45.18398860626900415, 28.73617430169818832, 5.000000000000000000 ) ) ;
#91262=EDGE_CURVE ( 'NONE', #141074, #114780, #73894, .T. ) ;
#91263=CARTESIAN_POINT ( 'NONE',  ( 32.99999999999977263, -3.485240976185046691, -4.108735105802321819 ) ) ;
#91264=DIRECTION ( 'NONE',  ( -0.000000000000000000, 0.000000000000000000, 1.000000000000000000 ) ) ;
#91266=PLANE ( 'NONE',  #9889 ) ;
#91269=ORIENTED_EDGE ( 'NONE', *, *, #37619, .T. ) ;
#91270=DIRECTION ( 'NONE',  ( -0.7071067811865486830, -0.7071067811865464625, 0.000000000000000000 ) ) ;
#91272=ORIENTED_EDGE ( 'NONE', *, *, #121688, .F. ) ;
#91273=VERTEX_POINT ( 'NONE', #104353 ) ;
#91274=LINE ( 'NONE', #135485, #102771 ) ;
#91275=ORIENTED_EDGE ( 'NONE', *, *, #21067, .T. ) ;
#91276=VECTOR ( 'NONE', #134999, 1000.000000000000000 ) ;
#91277=ADVANCED_FACE ( 'NONE', ( #107219 ), #51439, .F. ) ;
#91278=CARTESIAN_POINT ( 'NONE',  ( 25.49999999999982236, -11.56887692260770173, 4.000000000000000000 ) ) ;
#91279=DIRECTION ( 'NONE',  ( -0.000000000000000000, -0.3543493200069152138, 0.9351131265310292928 ) ) ;
#91280=AXIS2_PLACEMENT_3D ( 'NONE', #65436, #63982, #52374 ) ;
#91281=ADVANCED_FACE ( 'NONE', ( #28253 ), #61620, .F. ) ;
#91282=DIRECTION ( 'NONE',  ( -0.3543493200069162685, -0.000000000000000000, -0.9351131265310288487 ) ) ;
#91285=VERTEX_POINT ( 'NONE', #63047 ) ;
#91286=DIRECTION ( 'NONE',  ( -2.781805975412905890E-17, 0.3543493200069152693, 0.9351131265310292928 ) ) ;
#91289=EDGE_CURVE ( 'NONE', #137834, #11699, #5746, .T. ) ;
#91290=VECTOR ( 'NONE', #95886, 1000.000000000000000 ) ;
#91293=LINE ( 'NONE', #91968, #1869 ) ;
#91294=EDGE_CURVE ( 'NONE', #94085, #56955, #62320, .T. ) ;
#91295=PLANE ( 'NONE',  #18752 ) ;
#91297=VERTEX_POINT ( 'NONE', #118063 ) ;
#91298=ORIENTED_EDGE ( 'NONE', *, *, #44175, .T. ) ;
#91299=CARTESIAN_POINT ( 'NONE',  ( -33.13499573751602156, 3.759292476615678336, 15.36553568819733862 ) ) ;
#91300=DIRECTION ( 'NONE',  ( -0.7071067811865486830, 0.7071067811865464625, 0.000000000000000000 ) ) ;
#91301=DIRECTION ( 'NONE',  ( -0.000000000000000000, 0.000000000000000000, 1.000000000000000000 ) ) ;
#91302=CARTESIAN_POINT ( 'NONE',  ( 45.48921356237309510, -27.52281430457087197, 5.000000000000000000 ) ) ;
#91303=EDGE_LOOP ( 'NONE', ( #5042, #143469, #44371, #136403 ) ) ;
#91304=CARTESIAN_POINT ( 'NONE',  ( -39.18398860626899705, 28.73617430169814568, 5.000000000000000000 ) ) ;
#91305=EDGE_CURVE ( 'NONE', #120446, #77094, #95631, .T. ) ;
#91306=DIRECTION ( 'NONE',  ( -0.7071067811865486830, -0.7071067811865464625, 0.000000000000000000 ) ) ;
#91307=FACE_OUTER_BOUND ( 'NONE', #45701, .T. ) ;
#91308=ORIENTED_EDGE ( 'NONE', *, *, #92229, .F. ) ;
#91309=AXIS2_PLACEMENT_3D ( 'NONE', #133363, #96570, #74153 ) ;
#91310=EDGE_CURVE ( 'NONE', #103321, #104848, #18037, .T. ) ;
#91311=LINE ( 'NONE', #62963, #44789 ) ;
#91312=ORIENTED_EDGE ( 'NONE', *, *, #139111, .F. ) ;
#91314=ORIENTED_EDGE ( 'NONE', *, *, #51078, .F. ) ;
#91315=ORIENTED_EDGE ( 'NONE', *, *, #142390, .T. ) ;
#91316=CARTESIAN_POINT ( 'NONE',  ( 24.48921356237309510, -27.52281430457072631, 5.000000000000000000 ) ) ;
#91317=FACE_OUTER_BOUND ( 'NONE', #73592, .T. ) ;
#91318=EDGE_CURVE ( 'NONE', #79126, #83227, #39129, .T. ) ;
#91319=ORIENTED_EDGE ( 'NONE', *, *, #2451, .T. ) ;
#91321=LINE ( 'NONE', #115864, #28949 ) ;
#91322=DIRECTION ( 'NONE',  ( 0.000000000000000000, -1.000000000000000000, 0.000000000000000000 ) ) ;
#91323=DIRECTION ( 'NONE',  ( 0.7071067811865487940, 0.7071067811865463515, -0.000000000000000000 ) ) ;
#91324=LINE ( 'NONE', #80445, #94863 ) ;
#91325=DIRECTION ( 'NONE',  ( -0.7071067811865487940, 0.7071067811865463515, 0.000000000000000000 ) ) ;
#91326=DIRECTION ( 'NONE',  ( 0.7071067811865487940, 0.7071067811865463515, -0.000000000000000000 ) ) ;
#91327=FACE_OUTER_BOUND ( 'NONE', #856, .T. ) ;
#91328=ADVANCED_FACE ( 'NONE', ( #124170 ), #84767, .F. ) ;
#91329=DIRECTION ( 'NONE',  ( -0.000000000000000000, 0.3543493200069153248, 0.9351131265310291818 ) ) ;
#91331=CARTESIAN_POINT ( 'NONE',  ( 0.000000000000000000, 0.000000000000000000, 5.000000000000000000 ) ) ;
#91332=DIRECTION ( 'NONE',  ( -0.7071067811865486830, 0.7071067811865464625, 0.000000000000000000 ) ) ;
#91333=DIRECTION ( 'NONE',  ( 0.3543493200069162685, -0.000000000000000000, -0.9351131265310288487 ) ) ;
#91334=PLANE ( 'NONE',  #38497 ) ;
#91335=VERTEX_POINT ( 'NONE', #60924 ) ;
#91337=EDGE_CURVE ( 'NONE', #89964, #57727, #27508, .T. ) ;
#91339=EDGE_CURVE ( 'NONE', #96482, #64185, #75333, .T. ) ;
#91341=ORIENTED_EDGE ( 'NONE', *, *, #49505, .T. ) ;
#91342=VERTEX_POINT ( 'NONE', #131849 ) ;
#91343=VERTEX_POINT ( 'NONE', #31813 ) ;
#91344=LINE ( 'NONE', #113050, #29501 ) ;
#91345=LINE ( 'NONE', #135555, #18568 ) ;
#91347=ORIENTED_EDGE ( 'NONE', *, *, #100899, .T. ) ;
#91348=DIRECTION ( 'NONE',  ( -0.7071067811865487940, 0.7071067811865463515, 0.000000000000000000 ) ) ;
#91350=CARTESIAN_POINT ( 'NONE',  ( 0.6183849060199635428, -2.240707523384260824, 13.37739548510239196 ) ) ;
#91351=CARTESIAN_POINT ( 'NONE',  ( 21.79289321881330821, 9.759292476615618384, 5.000000000000000000 ) ) ;
#91352=DIRECTION ( 'NONE',  ( -0.7071067811865486830, -0.7071067811865464625, -0.000000000000000000 ) ) ;
#91354=CARTESIAN_POINT ( 'NONE',  ( 0.000000000000000000, 0.000000000000000000, 5.000000000000000000 ) ) ;
#91355=CARTESIAN_POINT ( 'NONE',  ( 21.87889065874226091, 8.431076354171498366, 5.000000000000000000 ) ) ;
#91356=CARTESIAN_POINT ( 'NONE',  ( 13.49999999999990408, 0.4311230773921762571, 4.000000000000000000 ) ) ;
#91357=CARTESIAN_POINT ( 'NONE',  ( 6.938893903907228378E-15, 17.58746187583906462, 4.000000000000000000 ) ) ;
#91358=VECTOR ( 'NONE', #58307, 1000.000000000000000 ) ;
#91360=CARTESIAN_POINT ( 'NONE',  ( 20.11162361894746553, 9.759292476615614831, 17.35367589129208099 ) ) ;
#91361=CARTESIAN_POINT ( 'NONE',  ( -19.17183060077633883, 21.75929247661549581, 4.000000000000000000 ) ) ;
#91363=PLANE ( 'NONE',  #21414 ) ;
#91364=EDGE_LOOP ( 'NONE', ( #92477, #75383, #124496, #98059 ) ) ;
#91365=ORIENTED_EDGE ( 'NONE', *, *, #88127, .T. ) ;
#91367=VERTEX_POINT ( 'NONE', #74622 ) ;
#91368=ADVANCED_FACE ( 'NONE', ( #42713 ), #22323, .F. ) ;
#91369=VECTOR ( 'NONE', #21426, 999.9999999999998863 ) ;
#91371=DIRECTION ( 'NONE',  ( -0.6830127018922181881, 0.6830127018922202975, -0.2588190451025214056 ) ) ;
#91372=EDGE_CURVE ( 'NONE', #103836, #15513, #33285, .T. ) ;
#91373=CARTESIAN_POINT ( 'NONE',  ( -32.99999999999975131, 20.58746187583903620, 4.000000000000000000 ) ) ;
#91374=DIRECTION ( 'NONE',  ( 0.7071067811865487940, 0.7071067811865463515, 0.000000000000000000 ) ) ;
#91376=AXIS2_PLACEMENT_3D ( 'NONE', #137472, #115663, #3349 ) ;
#91377=ORIENTED_EDGE ( 'NONE', *, *, #84816, .F. ) ;
#91378=EDGE_LOOP ( 'NONE', ( #24450, #39581, #121074, #56611 ) ) ;
#91382=ORIENTED_EDGE ( 'NONE', *, *, #120981, .T. ) ;
#91383=ORIENTED_EDGE ( 'NONE', *, *, #21136, .F. ) ;
#91384=LINE ( 'NONE', #58062, #86146 ) ;
#91386=AXIS2_PLACEMENT_3D ( 'NONE', #81291, #124768, #105842 ) ;
#91387=EDGE_CURVE ( 'NONE', #20150, #15770, #55011, .T. ) ;
#91389=VECTOR ( 'NONE', #37617, 1000.000000000000000 ) ;
#91391=EDGE_LOOP ( 'NONE', ( #78501, #106078, #47406, #106905 ) ) ;
#91392=ORIENTED_EDGE ( 'NONE', *, *, #4519, .T. ) ;
#91393=CARTESIAN_POINT ( 'NONE',  ( 14.99999999999989519, 13.93112307739203715, 4.000000000000000000 ) ) ;
#91394=EDGE_LOOP ( 'NONE', ( #2374, #71857, #117393, #60381 ) ) ;
#91396=DIRECTION ( 'NONE',  ( 0.6830127018922180770, -0.6830127018922204085, -0.2588190451025213501 ) ) ;
#91397=PLANE ( 'NONE',  #3478 ) ;
#91398=LINE ( 'NONE', #113834, #141441 ) ;
#91399=ORIENTED_EDGE ( 'NONE', *, *, #80699, .T. ) ;
#91400=CARTESIAN_POINT ( 'NONE',  ( 16.79601123714775213, -22.22500000000000142, -14.59902459068437786 ) ) ;
#91401=DIRECTION ( 'NONE',  ( -0.7071067811865486830, -0.7071067811865464625, 0.000000000000000000 ) ) ;
#91402=DIRECTION ( 'NONE',  ( -0.6830127018922180770, -0.6830127018922204085, -0.2588190451025213501 ) ) ;
#91403=FACE_BOUND ( 'NONE', #87271, .T. ) ;
#91404=VERTEX_POINT ( 'NONE', #99174 ) ;
#91406=DIRECTION ( 'NONE',  ( 0.7071067811865486830, -0.7071067811865464625, -0.000000000000000000 ) ) ;
#91407=ORIENTED_EDGE ( 'NONE', *, *, #45630, .T. ) ;
#91408=CARTESIAN_POINT ( 'NONE',  ( -9.005480084712511157, 28.92564299267931816, 4.000000000000000000 ) ) ;
#91410=ORIENTED_EDGE ( 'NONE', *, *, #124349, .F. ) ;
#91411=ORIENTED_EDGE ( 'NONE', *, *, #94911, .F. ) ;
#91413=VERTEX_POINT ( 'NONE', #142026 ) ;
#91414=CARTESIAN_POINT ( 'NONE',  ( 2.999999999999975575, 13.93112307739204425, 4.000000000000000000 ) ) ;
#91415=LINE ( 'NONE', #37012, #26528 ) ;
#91416=ORIENTED_EDGE ( 'NONE', *, *, #73479, .F. ) ;
#91417=CARTESIAN_POINT ( 'NONE',  ( -44.99451991528749772, 28.92564299267969474, 4.000000000000000000 ) ) ;
#91418=VECTOR ( 'NONE', #48614, 1000.000000000000000 ) ;
#91419=DIRECTION ( 'NONE',  ( -0.000000000000000000, 0.000000000000000000, 1.000000000000000000 ) ) ;
#91422=ORIENTED_EDGE ( 'NONE', *, *, #129605, .F. ) ;
#91423=ADVANCED_FACE ( 'NONE', ( #20193 ), #76777, .F. ) ;
#91424=ORIENTED_EDGE ( 'NONE', *, *, #113275, .F. ) ;
#91425=ORIENTED_EDGE ( 'NONE', *, *, #71671, .T. ) ;
#91427=DIRECTION ( 'NONE',  ( -0.000000000000000000, -0.3543493200069152693, 0.9351131265310292928 ) ) ;
#91428=ORIENTED_EDGE ( 'NONE', *, *, #135517, .F. ) ;
#91429=ADVANCED_FACE ( 'NONE', ( #77487 ), #118811, .F. ) ;
#91430=EDGE_CURVE ( 'NONE', #80319, #20411, #132592, .T. ) ;
#91431=ORIENTED_EDGE ( 'NONE', *, *, #66270, .F. ) ;
#91432=FACE_OUTER_BOUND ( 'NONE', #57449, .T. ) ;
#91433=EDGE_CURVE ( 'NONE', #132258, #114780, #43406, .T. ) ;
#91434=EDGE_CURVE ( 'NONE', #112333, #2363, #30384, .T. ) ;
#91435=CARTESIAN_POINT ( 'NONE',  ( 33.18398860626899705, 28.73617430169810305, 5.000000000000000000 ) ) ;
#91437=LINE ( 'NONE', #124763, #18613 ) ;
#91438=ORIENTED_EDGE ( 'NONE', *, *, #41882, .F. ) ;
#91440=ADVANCED_FACE ( 'NONE', ( #65180 ), #107907, .F. ) ;
#91441=EDGE_CURVE ( 'NONE', #138495, #113729, #52822, .T. ) ;
#91442=VECTOR ( 'NONE', #89722, 1000.000000000000000 ) ;
#91445=EDGE_LOOP ( 'NONE', ( #124010, #103478, #130202, #47569 ) ) ;
#91447=CARTESIAN_POINT ( 'NONE',  ( 24.29974487139158867, -27.71228299555223273, 4.000000000000000000 ) ) ;
#91448=AXIS2_PLACEMENT_3D ( 'NONE', #22284, #143382, #44843 ) ;
#91449=EDGE_CURVE ( 'NONE', #16533, #103400, #31115, .T. ) ;
#91450=CARTESIAN_POINT ( 'NONE',  ( -7.499999999999944045, 0.05218569542916710879, 5.000000000000000000 ) ) ;
#91452=ORIENTED_EDGE ( 'NONE', *, *, #27243, .F. ) ;
#91453=CARTESIAN_POINT ( 'NONE',  ( 35.53839644629407246, -9.740707523384177335, 17.74957260769619083 ) ) ;
#91454=ORIENTED_EDGE ( 'NONE', *, *, #46477, .T. ) ;
#91455=LINE ( 'NONE', #100187, #120367 ) ;
#91456=LINE ( 'NONE', #135670, #69500 ) ;
#91457=CARTESIAN_POINT ( 'NONE',  ( 4.499999999999962697, -14.70932175296476352, -11.46312253303838347 ) ) ;
#91458=CARTESIAN_POINT ( 'NONE',  ( -8.292893218813397027, 17.25929247661554911, 5.000000000000000000 ) ) ;
#91459=DIRECTION ( 'NONE',  ( 0.6830127018922180770, -0.6830127018922204085, -0.2588190451025213501 ) ) ;
#91460=VERTEX_POINT ( 'NONE', #21655 ) ;
#91462=VECTOR ( 'NONE', #17972, 1000.000000000000227 ) ;
#91463=CARTESIAN_POINT ( 'NONE',  ( -19.05000000000000071, 3.174999999999997158, 4.000000000000000000 ) ) ;
#91464=FACE_OUTER_BOUND ( 'NONE', #79158, .T. ) ;
#91465=ORIENTED_EDGE ( 'NONE', *, *, #108245, .F. ) ;
#91467=CARTESIAN_POINT ( 'NONE',  ( -28.49999999999981171, 16.18958161055400069, -11.56426086740817638 ) ) ;
#91468=ORIENTED_EDGE ( 'NONE', *, *, #108949, .F. ) ;
#91470=ORIENTED_EDGE ( 'NONE', *, *, #84173, .F. ) ;
#91471=VERTEX_POINT ( 'NONE', #110765 ) ;
#91473=CARTESIAN_POINT ( 'NONE',  ( 29.99999999999979039, 5.966399257802205369, 5.000000000000000000 ) ) ;
#91475=VERTEX_POINT ( 'NONE', #70205 ) ;
#91478=AXIS2_PLACEMENT_3D ( 'NONE', #3154, #99605, #69159 ) ;
#91479=VECTOR ( 'NONE', #50591, 1000.000000000000000 ) ;
#91480=DIRECTION ( 'NONE',  ( -0.3543493200069162685, -0.000000000000000000, -0.9351131265310288487 ) ) ;
#91481=ORIENTED_EDGE ( 'NONE', *, *, #92229, .T. ) ;
#91482=VECTOR ( 'NONE', #6312, 1000.000000000000000 ) ;
#91483=LINE ( 'NONE', #66872, #16521 ) ;
#91484=LINE ( 'NONE', #69025, #42154 ) ;
#91488=LINE ( 'NONE', #38526, #59927 ) ;
#91489=LINE ( 'NONE', #125550, #90547 ) ;
#91490=LINE ( 'NONE', #125551, #61601 ) ;
#91491=ORIENTED_EDGE ( 'NONE', *, *, #128422, .T. ) ;
#91492=ORIENTED_EDGE ( 'NONE', *, *, #100509, .F. ) ;
#91496=ORIENTED_EDGE ( 'NONE', *, *, #48602, .T. ) ;
#91499=ORIENTED_EDGE ( 'NONE', *, *, #108077, .F. ) ;
#91501=LINE ( 'NONE', #24791, #92573 ) ;
#91502=VERTEX_POINT ( 'NONE', #36115 ) ;
#91504=PLANE ( 'NONE',  #72234 ) ;
#91505=EDGE_CURVE ( 'NONE', #89689, #79010, #91893, .T. ) ;
#91506=DIRECTION ( 'NONE',  ( 0.6830127018922181881, 0.6830127018922202975, -0.2588190451025214056 ) ) ;
#91507=FACE_OUTER_BOUND ( 'NONE', #73420, .T. ) ;
#91509=ORIENTED_EDGE ( 'NONE', *, *, #105500, .F. ) ;
#91510=DIRECTION ( 'NONE',  ( 0.6830127018922180770, -0.6830127018922204085, -0.2588190451025213501 ) ) ;
#91511=CARTESIAN_POINT ( 'NONE',  ( 4.499999999999969802, -13.53360074219760101, 5.000000000000000000 ) ) ;
#91513=EDGE_CURVE ( 'NONE', #52437, #110391, #56472, .T. ) ;
#91514=CARTESIAN_POINT ( 'NONE',  ( -8.999999999999937828, 13.93112307739204603, 4.000000000000000000 ) ) ;
#91515=DIRECTION ( 'NONE',  ( 0.7071067811865487940, 0.7071067811865463515, 0.000000000000000000 ) ) ;
#91518=LINE ( 'NONE', #80648, #110889 ) ;
#91519=ORIENTED_EDGE ( 'NONE', *, *, #22109, .T. ) ;
#91520=VERTEX_POINT ( 'NONE', #68066 ) ;
#91522=VERTEX_POINT ( 'NONE', #113643 ) ;
#91523=ORIENTED_EDGE ( 'NONE', *, *, #6979, .F. ) ;
#91524=EDGE_CURVE ( 'NONE', #5899, #126135, #1296, .T. ) ;
#91525=PLANE ( 'NONE',  #78446 ) ;
#91526=LINE ( 'NONE', #3066, #101013 ) ;
#91527=VERTEX_POINT ( 'NONE', #79660 ) ;
#91528=DIRECTION ( 'NONE',  ( -0.7071067811865486830, -0.7071067811865464625, -0.000000000000000000 ) ) ;
#91529=DIRECTION ( 'NONE',  ( -0.000000000000000000, 0.3543493200069153248, 0.9351131265310292928 ) ) ;
#91531=EDGE_CURVE ( 'NONE', #91750, #87099, #69461, .T. ) ;
#91533=DIRECTION ( 'NONE',  ( -0.6830127018922181881, 0.6830127018922202975, -0.2588190451025214056 ) ) ;
#91534=ORIENTED_EDGE ( 'NONE', *, *, #40080, .F. ) ;
#91535=LINE ( 'NONE', #45900, #109869 ) ;
#91536=CARTESIAN_POINT ( 'NONE',  ( 60.18398860626900415, 28.73617430169829490, 5.000000000000000000 ) ) ;
#91538=( BOUNDED_CURVE ( )  B_SPLINE_CURVE ( 3, ( #130190, #64214, #97532, #52605 ),
 .UNSPECIFIED., .F., .F. ) 
 B_SPLINE_CURVE_WITH_KNOTS ( ( 4, 4 ),
 ( 5.920967161967926273, 7.341195215986594746 ),
 .UNSPECIFIED. ) 
 CURVE ( )  GEOMETRIC_REPRESENTATION_ITEM ( )  RATIONAL_B_SPLINE_CURVE ( ( 1.000000000000000000, 0.8388583629366703764, 0.8388583629366703764, 1.000000000000000000 ) ) 
 REPRESENTATION_ITEM ( '' )  );
#91539=LINE ( 'NONE', #100268, #7070 ) ;
#91540=VERTEX_POINT ( 'NONE', #23797 ) ;
#91541=EDGE_CURVE ( 'NONE', #117995, #104048, #111509, .T. ) ;
#91542=ORIENTED_EDGE ( 'NONE', *, *, #108238, .T. ) ;
#91544=CARTESIAN_POINT ( 'NONE',  ( -30.70701326429283640, -21.74070752338405654, 4.999753212805224223 ) ) ;
#91545=CARTESIAN_POINT ( 'NONE',  ( 10.17183060077640633, -20.24070752338407075, 4.000000000000000000 ) ) ;
#91546=LINE ( 'NONE', #124163, #94922 ) ;
#91547=FACE_OUTER_BOUND ( 'NONE', #10861, .T. ) ;
#91548=VECTOR ( 'NONE', #138062, 1000.000000000000000 ) ;
#91550=AXIS2_PLACEMENT_3D ( 'NONE', #93139, #25731, #47546 ) ;
#91552=CARTESIAN_POINT ( 'NONE',  ( 27.48921356237309155, -27.52281430457074762, 5.000000000000000000 ) ) ;
#91553=ORIENTED_EDGE ( 'NONE', *, *, #132966, .T. ) ;
#91554=EDGE_LOOP ( 'NONE', ( #51316, #92138, #85341, #59406 ) ) ;
#91555=DIRECTION ( 'NONE',  ( 0.000000000000000000, 0.000000000000000000, 1.000000000000000000 ) ) ;
#91556=VERTEX_POINT ( 'NONE', #100650 ) ;
#91559=VECTOR ( 'NONE', #72444, 1000.000000000000000 ) ;
#91560=CARTESIAN_POINT ( 'NONE',  ( 27.45983838949723221, 18.75929247661552068, 8.305906642995550371 ) ) ;
#91563=FACE_BOUND ( 'NONE', #143151, .T. ) ;
#91565=LINE ( 'NONE', #114712, #15529 ) ;
#91566=CARTESIAN_POINT ( 'NONE',  ( -5.700255128608413102, -27.71228299555201957, 4.000000000000000000 ) ) ;
#91568=CARTESIAN_POINT ( 'NONE',  ( 34.49999999999976552, -4.535744391599457082, 4.994342998332164107 ) ) ;
#91569=ORIENTED_EDGE ( 'NONE', *, *, #65723, .F. ) ;
#91570=DIRECTION ( 'NONE',  ( -0.6830127018922180770, -0.6830127018922204085, -0.2588190451025213501 ) ) ;
#91571=VECTOR ( 'NONE', #53539, 1000.000000000000000 ) ;
#91572=ORIENTED_EDGE ( 'NONE', *, *, #20739, .F. ) ;
#91573=AXIS2_PLACEMENT_3D ( 'NONE', #32328, #110560, #98981 ) ;
#91576=ORIENTED_EDGE ( 'NONE', *, *, #123548, .T. ) ;
#91578=CARTESIAN_POINT ( 'NONE',  ( 34.77149322861314573, 20.25929247661551358, 7.808871592221849234 ) ) ;
#91579=ORIENTED_EDGE ( 'NONE', *, *, #121653, .F. ) ;
#91580=CARTESIAN_POINT ( 'NONE',  ( 36.48921356237310221, -27.52281430457080802, 5.000000000000000000 ) ) ;
#91581=ADVANCED_FACE ( 'NONE', ( #27335 ), #92594, .F. ) ;
#91582=DIRECTION ( 'NONE',  ( 0.6830127018922181881, 0.6830127018922202975, -0.2588190451025214056 ) ) ;
#91584=CARTESIAN_POINT ( 'NONE',  ( -26.99999999999980105, 1.931123077392163712, 4.000000000000000000 ) ) ;
#91585=PLANE ( 'NONE',  #95924 ) ;
#91586=CARTESIAN_POINT ( 'NONE',  ( 31.17183060077625711, 3.759292476615683665, 4.000000000000000000 ) ) ;
#91587=DIRECTION ( 'NONE',  ( -0.000000000000000000, 0.000000000000000000, 1.000000000000000000 ) ) ;
#91588=ORIENTED_EDGE ( 'NONE', *, *, #62945, .F. ) ;
#91589=VERTEX_POINT ( 'NONE', #29479 ) ;
#91590=CARTESIAN_POINT ( 'NONE',  ( 33.18398860626899705, 28.73617430169810305, 5.000000000000000000 ) ) ;
#91592=EDGE_LOOP ( 'NONE', ( #76756, #5035, #18909, #95850, #76941 ) ) ;
#91593=VERTEX_POINT ( 'NONE', #17870 ) ;
#91594=ORIENTED_EDGE ( 'NONE', *, *, #105814, .T. ) ;
#91596=DIRECTION ( 'NONE',  ( -1.000000000000000000, 0.000000000000000000, -0.000000000000000000 ) ) ;
#91597=ORIENTED_EDGE ( 'NONE', *, *, #134903, .T. ) ;
#91598=CARTESIAN_POINT ( 'NONE',  ( 12.42327845806345721, 11.25929247661559529, 17.85071094206581321 ) ) ;
#91600=EDGE_CURVE ( 'NONE', #50386, #31310, #125973, .T. ) ;
#91601=EDGE_CURVE ( 'NONE', #119206, #109845, #38950, .T. ) ;
#91603=FACE_OUTER_BOUND ( 'NONE', #45789, .T. ) ;
#91606=LINE ( 'NONE', #125675, #135983 ) ;
#91607=EDGE_CURVE ( 'NONE', #127807, #20442, #50538, .T. ) ;
#91608=DIRECTION ( 'NONE',  ( -0.7071067811865487940, 0.7071067811865463515, -0.000000000000000000 ) ) ;
#91609=DIRECTION ( 'NONE',  ( -0.7071067811865487940, 0.7071067811865463515, -0.000000000000000000 ) ) ;
#91610=CARTESIAN_POINT ( 'NONE',  ( 34.92499999999998295, 8.454535441273616669, -0.2181437882982223408 ) ) ;
#91611=ORIENTED_EDGE ( 'NONE', *, *, #38412, .F. ) ;
#91612=VERTEX_POINT ( 'NONE', #117889 ) ;
#91613=EDGE_CURVE ( 'NONE', #118849, #110220, #84606, .T. ) ;
#91614=LINE ( 'NONE', #35846, #61209 ) ;
#91616=CARTESIAN_POINT ( 'NONE',  ( 3.299744871391591339, -27.71228299555208352, 4.000000000000000000 ) ) ;
#91617=VERTEX_POINT ( 'NONE', #49137 ) ;
#91618=DIRECTION ( 'NONE',  ( -0.000000000000000000, 0.3543493200069153248, 0.9351131265310291818 ) ) ;
#91619=LINE ( 'NONE', #46747, #101208 ) ;
#91620=EDGE_CURVE ( 'NONE', #54976, #15318, #136828, .T. ) ;
#91623=DIRECTION ( 'NONE',  ( 0.7071067811865486830, -0.7071067811865464625, -0.000000000000000000 ) ) ;
#91624=ORIENTED_EDGE ( 'NONE', *, *, #26972, .F. ) ;
#91628=EDGE_CURVE ( 'NONE', #24049, #89715, #104913, .T. ) ;
#91629=LINE ( 'NONE', #125703, #132783 ) ;
#91631=EDGE_CURVE ( 'NONE', #21885, #55035, #5581, .T. ) ;
#91632=VERTEX_POINT ( 'NONE', #60004 ) ;
#91633=EDGE_LOOP ( 'NONE', ( #130688, #79900, #56681, #135117 ) ) ;
#91635=DIRECTION ( 'NONE',  ( 0.7071067811865487940, 0.7071067811865463515, -0.000000000000000000 ) ) ;
#91636=EDGE_CURVE ( 'NONE', #77481, #22051, #28801, .T. ) ;
#91638=VECTOR ( 'NONE', #83830, 999.9999999999998863 ) ;
#91639=CARTESIAN_POINT ( 'NONE',  ( 26.99451991528749417, 28.92564299267956685, 4.000000000000000000 ) ) ;
#91640=LINE ( 'NONE', #46018, #90080 ) ;
#91641=LINE ( 'NONE', #14789, #131711 ) ;
#91642=LINE ( 'NONE', #6014, #130129 ) ;
#91644=ORIENTED_EDGE ( 'NONE', *, *, #64070, .T. ) ;
#91645=CARTESIAN_POINT ( 'NONE',  ( 8.999999999999941380, 4.552185695429119328, 5.000000000000000000 ) ) ;
#91646=LINE ( 'NONE', #134453, #131556 ) ;
#91648=DIRECTION ( 'NONE',  ( -0.000000000000000000, 0.3543493200069153248, 0.9351131265310292928 ) ) ;
#91650=ORIENTED_EDGE ( 'NONE', *, *, #31380, .F. ) ;
#91651=VECTOR ( 'NONE', #49321, 1000.000000000000000 ) ;
#91652=DIRECTION ( 'NONE',  ( 0.7071067811865487940, 0.7071067811865463515, -0.000000000000000000 ) ) ;
#91653=ADVANCED_FACE ( 'NONE', ( #51265 ), #95460, .F. ) ;
#91654=VERTEX_POINT ( 'NONE', #127375 ) ;
#91655=CARTESIAN_POINT ( 'NONE',  ( -39.18398860626899705, 28.73617430169814568, 5.000000000000000000 ) ) ;
#91656=FACE_OUTER_BOUND ( 'NONE', #138278, .T. ) ;
#91657=FACE_OUTER_BOUND ( 'NONE', #60347, .T. ) ;
#91658=CARTESIAN_POINT ( 'NONE',  ( 3.299744871391591339, -27.71228299555208352, 4.000000000000000000 ) ) ;
#91659=CARTESIAN_POINT ( 'NONE',  ( 42.48921356237308800, -27.52281430457085065, 5.000000000000000000 ) ) ;
#91660=ORIENTED_EDGE ( 'NONE', *, *, #91505, .T. ) ;
#91661=ORIENTED_EDGE ( 'NONE', *, *, #47878, .F. ) ;
#91662=CARTESIAN_POINT ( 'NONE',  ( -18.79289321881331887, 9.759292476615614831, 5.000000000000000000 ) ) ;
#91664=CARTESIAN_POINT ( 'NONE',  ( -21.29974487139158512, -27.71228299555221142, 4.000000000000000000 ) ) ;
#91666=VECTOR ( 'NONE', #115719, 1000.000000000000000 ) ;
#91669=VECTOR ( 'NONE', #24132, 1000.000000000000227 ) ;
#91670=DIRECTION ( 'NONE',  ( -4.681814790819591790E-17, -0.3543493200069152693, 0.9351131265310292928 ) ) ;
#91671=ORIENTED_EDGE ( 'NONE', *, *, #86390, .F. ) ;
#91674=CARTESIAN_POINT ( 'NONE',  ( -15.29974487139158867, -27.71228299555216879, 4.000000000000000000 ) ) ;
#91676=EDGE_CURVE ( 'NONE', #96881, #135052, #116510, .T. ) ;
#91677=DIRECTION ( 'NONE',  ( 0.3543493200069163240, -0.000000000000000000, 0.9351131265310288487 ) ) ;
#91678=VECTOR ( 'NONE', #66708, 999.9999999999998863 ) ;
#91679=ORIENTED_EDGE ( 'NONE', *, *, #80076, .F. ) ;
#91680=DIRECTION ( 'NONE',  ( 0.7071067811865487940, 0.7071067811865463515, 0.000000000000000000 ) ) ;
#91681=EDGE_CURVE ( 'NONE', #65370, #76484, #105601, .T. ) ;
#91682=DIRECTION ( 'NONE',  ( -0.7071067811865487940, 0.7071067811865463515, 0.000000000000000000 ) ) ;
#91684=DIRECTION ( 'NONE',  ( -0.6830127018922180770, -0.6830127018922204085, -0.2588190451025213501 ) ) ;
#91685=ORIENTED_EDGE ( 'NONE', *, *, #123402, .F. ) ;
#91687=CARTESIAN_POINT ( 'NONE',  ( 9.707106781186483957, 2.259292476615696099, 5.000000000000000000 ) ) ;
#91688=CARTESIAN_POINT ( 'NONE',  ( 12.29974487139158512, -27.71228299555214747, 4.000000000000000000 ) ) ;
#91690=EDGE_CURVE ( 'NONE', #79341, #31148, #128115, .T. ) ;
#91691=CARTESIAN_POINT ( 'NONE',  ( 33.79289321881321939, -11.24070752338417023, 5.000000000000000000 ) ) ;
#91692=LINE ( 'NONE', #14120, #17424 ) ;
#91693=EDGE_LOOP ( 'NONE', ( #94710, #21396, #84501, #37694 ) ) ;
#91694=FACE_OUTER_BOUND ( 'NONE', #137368, .T. ) ;
#91695=DIRECTION ( 'NONE',  ( -1.000000000000000000, 0.000000000000000000, 0.000000000000000000 ) ) ;
#91696=CARTESIAN_POINT ( 'NONE',  ( -36.48921356237310221, -27.52281430457080802, 5.000000000000000000 ) ) ;
#91697=FACE_OUTER_BOUND ( 'NONE', #68327, .T. ) ;
#91698=ORIENTED_EDGE ( 'NONE', *, *, #34780, .F. ) ;
#91699=ORIENTED_EDGE ( 'NONE', *, *, #77951, .F. ) ;
#91701=ORIENTED_EDGE ( 'NONE', *, *, #139529, .F. ) ;
#91702=FACE_OUTER_BOUND ( 'NONE', #115509, .T. ) ;
#91703=PLANE ( 'NONE',  #29491 ) ;
#91704=CARTESIAN_POINT ( 'NONE',  ( 34.91107144025653497, 21.84219451764873909, 4.000000000000000000 ) ) ;
#91706=LINE ( 'NONE', #14855, #52423 ) ;
#91707=VERTEX_POINT ( 'NONE', #108440 ) ;
#91708=VERTEX_POINT ( 'NONE', #30205 ) ;
#91709=AXIS2_PLACEMENT_3D ( 'NONE', #102416, #124852, #36425 ) ;
#91710=LINE ( 'NONE', #36612, #104720 ) ;
#91712=ADVANCED_FACE ( 'NONE', ( #43247 ), #132426, .F. ) ;
#91713=ORIENTED_EDGE ( 'NONE', *, *, #43133, .F. ) ;
#91714=EDGE_CURVE ( 'NONE', #32886, #133889, #77326, .T. ) ;
#91716=ORIENTED_EDGE ( 'NONE', *, *, #62800, .T. ) ;
#91717=CARTESIAN_POINT ( 'NONE',  ( 24.18398860626899705, 28.73617430169804265, 5.000000000000000000 ) ) ;
#91718=DIRECTION ( 'NONE',  ( -0.7071067811865486830, -0.7071067811865464625, -0.000000000000000000 ) ) ;
#91719=ORIENTED_EDGE ( 'NONE', *, *, #69792, .F. ) ;
#91720=FACE_BOUND ( 'NONE', #103795, .T. ) ;
#91721=EDGE_CURVE ( 'NONE', #81979, #7814, #64272, .T. ) ;
#91722=LINE ( 'NONE', #112069, #57209 ) ;
#91723=DIRECTION ( 'NONE',  ( -2.781805975412905890E-17, 0.3543493200069152693, 0.9351131265310292928 ) ) ;
#91725=CARTESIAN_POINT ( 'NONE',  ( 2.816011393730999401, 28.73617430169785436, 5.000000000000000000 ) ) ;
#91729=VECTOR ( 'NONE', #140258, 1000.000000000000000 ) ;
#91730=VERTEX_POINT ( 'NONE', #74452 ) ;
#91731=EDGE_LOOP ( 'NONE', ( #54624, #119857, #103633, #39928 ) ) ;
#91733=VERTEX_POINT ( 'NONE', #109192 ) ;
#91734=VECTOR ( 'NONE', #16447, 1000.000000000000000 ) ;
#91735=DIRECTION ( 'NONE',  ( -0.7071067811865486830, -0.7071067811865464625, -0.000000000000000000 ) ) ;
#91736=DIRECTION ( 'NONE',  ( -0.7071067811865486830, 0.7071067811865464625, 0.000000000000000000 ) ) ;
#91738=CARTESIAN_POINT ( 'NONE',  ( 36.48921356237310221, -27.52281430457080802, 5.000000000000000000 ) ) ;
#91740=DIRECTION ( 'NONE',  ( 0.6830127018922181881, 0.6830127018922202975, -0.2588190451025214056 ) ) ;
#91741=CARTESIAN_POINT ( 'NONE',  ( -33.79289321881321939, -14.24070752338414003, 5.000000000000000000 ) ) ;
#91742=VECTOR ( 'NONE', #83352, 1000.000000000000000 ) ;
#91743=CARTESIAN_POINT ( 'NONE',  ( -18.48921356237309510, -27.52281430457068367, 5.000000000000000000 ) ) ;
#91745=FACE_OUTER_BOUND ( 'NONE', #75832, .T. ) ;
#91747=ORIENTED_EDGE ( 'NONE', *, *, #123761, .F. ) ;
#91748=DIRECTION ( 'NONE',  ( -0.6830127018922181881, 0.6830127018922202975, -0.2588190451025214056 ) ) ;
#91749=CARTESIAN_POINT ( 'NONE',  ( -18.31657961132778212, -6.740707523384209310, 11.88629033278128588 ) ) ;
#91750=VERTEX_POINT ( 'NONE', #85285 ) ;
#91752=ORIENTED_EDGE ( 'NONE', *, *, #111619, .F. ) ;
#91755=ORIENTED_EDGE ( 'NONE', *, *, #107848, .T. ) ;
#91756=VECTOR ( 'NONE', #24844, 1000.000000000000227 ) ;
#91757=VECTOR ( 'NONE', #143066, 1000.000000000000000 ) ;
#91758=AXIS2_PLACEMENT_3D ( 'NONE', #115927, #15195, #59472 ) ;
#91759=EDGE_CURVE ( 'NONE', #53420, #102617, #22165, .T. ) ;
#91761=VERTEX_POINT ( 'NONE', #20027 ) ;
#91763=DIRECTION ( 'NONE',  ( 0.7071067811865486830, -0.7071067811865464625, -0.000000000000000000 ) ) ;
#91764=EDGE_CURVE ( 'NONE', #90219, #109971, #32361, .T. ) ;
#91765=EDGE_LOOP ( 'NONE', ( #846, #78658, #108477, #113718 ) ) ;
#91766=CARTESIAN_POINT ( 'NONE',  ( -30.18398860626900060, 28.73617430169808173, 5.000000000000000000 ) ) ;
#91767=VECTOR ( 'NONE', #141975, 1000.000000000000000 ) ;
#91770=ORIENTED_EDGE ( 'NONE', *, *, #99790, .T. ) ;
#91771=EDGE_CURVE ( 'NONE', #17205, #89689, #97593, .T. ) ;
#91772=DIRECTION ( 'NONE',  ( 0.7071067811865487940, -0.7071067811865463515, 0.000000000000000000 ) ) ;
#91773=CARTESIAN_POINT ( 'NONE',  ( 81.48921356237309510, -27.52281430457112066, 5.000000000000000000 ) ) ;
#91775=ORIENTED_EDGE ( 'NONE', *, *, #10546, .T. ) ;
#91776=CARTESIAN_POINT ( 'NONE',  ( 18.70701326429291456, -21.74070752338405654, 4.999753212805210012 ) ) ;
#91777=ORIENTED_EDGE ( 'NONE', *, *, #104560, .T. ) ;
#91778=EDGE_LOOP ( 'NONE', ( #85925, #33236, #70652, #37838 ) ) ;
#91779=ORIENTED_EDGE ( 'NONE', *, *, #70567, .T. ) ;
#91780=DIRECTION ( 'NONE',  ( -0.7071067811865486830, -0.7071067811865464625, 0.000000000000000000 ) ) ;
#91782=ADVANCED_FACE ( 'NONE', ( #86752 ), #130972, .F. ) ;
#91783=DIRECTION ( 'NONE',  ( 0.6830127018922181881, 0.6830127018922202975, -0.2588190451025214056 ) ) ;
#91784=DIRECTION ( 'NONE',  ( 0.000000000000000000, -1.000000000000000000, 0.000000000000000000 ) ) ;
#91786=LINE ( 'NONE', #102689, #30339 ) ;
#91787=VERTEX_POINT ( 'NONE', #120776 ) ;
#91788=EDGE_CURVE ( 'NONE', #108392, #27000, #21486, .T. ) ;
#91790=CARTESIAN_POINT ( 'NONE',  ( 0.000000000000000000, 0.000000000000000000, 5.000000000000000000 ) ) ;
#91791=DIRECTION ( 'NONE',  ( 0.6830127018922181881, 0.6830127018922202975, -0.2588190451025214056 ) ) ;
#91792=DIRECTION ( 'NONE',  ( -0.000000000000000000, 0.3543493200069153248, 0.9351131265310292928 ) ) ;
#91793=ORIENTED_EDGE ( 'NONE', *, *, #104405, .F. ) ;
#91794=VERTEX_POINT ( 'NONE', #10572 ) ;
#91795=ORIENTED_EDGE ( 'NONE', *, *, #121448, .T. ) ;
#91796=CARTESIAN_POINT ( 'NONE',  ( 14.27718569542929572, -21.72500000000000142, 5.000000000000000000 ) ) ;
#91797=DIRECTION ( 'NONE',  ( 0.7071067811865487940, 0.7071067811865463515, 0.000000000000000000 ) ) ;
#91798=ADVANCED_FACE ( 'NONE', ( #107752 ), #99016, .F. ) ;
#91799=DIRECTION ( 'NONE',  ( 0.6830127018922181881, 0.6830127018922202975, -0.2588190451025214056 ) ) ;
#91801=LINE ( 'NONE', #37447, #79909 ) ;
#91802=CARTESIAN_POINT ( 'NONE',  ( -42.48921356237308800, -27.52281430457085065, 5.000000000000000000 ) ) ;
#91803=CARTESIAN_POINT ( 'NONE',  ( 26.29289321881326913, 20.25929247661551713, 5.000000000000000000 ) ) ;
#91804=LINE ( 'NONE', #4743, #138985 ) ;
#91805=DIRECTION ( 'NONE',  ( -0.000000000000000000, 0.3543493200069153248, 0.9351131265310292928 ) ) ;
#91806=DIRECTION ( 'NONE',  ( -0.7071067811865486830, -0.7071067811865464625, 0.000000000000000000 ) ) ;
#91807=LINE ( 'NONE', #137480, #99915 ) ;
#91808=CARTESIAN_POINT ( 'NONE',  ( 36.48921356237310221, -27.52281430457080802, 5.000000000000000000 ) ) ;
#91809=LINE ( 'NONE', #135355, #141444 ) ;
#91810=EDGE_CURVE ( 'NONE', #107864, #63125, #52668, .T. ) ;
#91812=ORIENTED_EDGE ( 'NONE', *, *, #66273, .F. ) ;
#91814=VERTEX_POINT ( 'NONE', #41808 ) ;
#91815=DIRECTION ( 'NONE',  ( -0.7071067811865486830, -0.7071067811865464625, 0.000000000000000000 ) ) ;
#91816=LINE ( 'NONE', #57803, #90392 ) ;
#91817=ORIENTED_EDGE ( 'NONE', *, *, #89180, .F. ) ;
#91818=VECTOR ( 'NONE', #133468, 1000.000000000000000 ) ;
#91819=CARTESIAN_POINT ( 'NONE',  ( 39.48921356237310221, -27.52281430457082934, 5.000000000000000000 ) ) ;
#91821=ORIENTED_EDGE ( 'NONE', *, *, #103825, .T. ) ;
#91822=LINE ( 'NONE', #135367, #53046 ) ;
#91823=EDGE_LOOP ( 'NONE', ( #47410, #142909, #87242, #97530 ) ) ;
#91825=ORIENTED_EDGE ( 'NONE', *, *, #97169, .F. ) ;
#91826=CARTESIAN_POINT ( 'NONE',  ( 15.18398860626900237, 28.73617430169797871, 5.000000000000000000 ) ) ;
#91827=EDGE_CURVE ( 'NONE', #3834, #112546, #86022, .T. ) ;
#91828=VECTOR ( 'NONE', #13993, 999.9999999999998863 ) ;
#91831=DIRECTION ( 'NONE',  ( 0.7071067811865486830, -0.7071067811865464625, -0.000000000000000000 ) ) ;
#91833=VECTOR ( 'NONE', #23613, 999.9999999999998863 ) ;
#91834=LINE ( 'NONE', #136059, #28747 ) ;
#91835=DIRECTION ( 'NONE',  ( 0.7071067811865486830, -0.7071067811865464625, -0.000000000000000000 ) ) ;
#91838=CARTESIAN_POINT ( 'NONE',  ( -9.838293875473743455, -6.740707523384205757, 16.75550250614864822 ) ) ;
#91840=LINE ( 'NONE', #25880, #36227 ) ;
#91841=VERTEX_POINT ( 'NONE', #99744 ) ;
#91842=DIRECTION ( 'NONE',  ( -0.7071067811865487940, 0.7071067811865463515, 0.000000000000000000 ) ) ;
#91843=ORIENTED_EDGE ( 'NONE', *, *, #31053, .F. ) ;
#91844=ADVANCED_FACE ( 'NONE', ( #78721 ), #47564, .F. ) ;
#91846=FACE_OUTER_BOUND ( 'NONE', #110027, .T. ) ;
#91847=LINE ( 'NONE', #73512, #76155 ) ;
#91849=DIRECTION ( 'NONE',  ( 0.6830127018922180770, -0.6830127018922204085, -0.2588190451025213501 ) ) ;
#91853=VECTOR ( 'NONE', #88885, 1000.000000000000000 ) ;
#91854=ORIENTED_EDGE ( 'NONE', *, *, #10607, .T. ) ;
#91855=EDGE_CURVE ( 'NONE', #49148, #89661, #12009, .T. ) ;
#91856=PLANE ( 'NONE',  #84170 ) ;
#91858=ORIENTED_EDGE ( 'NONE', *, *, #81799, .T. ) ;
#91859=CARTESIAN_POINT ( 'NONE',  ( -10.36246187583893175, 22.22500000000000853, 4.000000000000000000 ) ) ;
#91860=DIRECTION ( 'NONE',  ( -0.3543493200069162685, -0.000000000000000000, -0.9351131265310288487 ) ) ;
#91861=DIRECTION ( 'NONE',  ( 1.000000000000000000, 0.000000000000000000, 0.000000000000000000 ) ) ;
#91862=AXIS2_PLACEMENT_3D ( 'NONE', #21100, #87791, #121124 ) ;
#91864=VECTOR ( 'NONE', #26818, 1000.000000000000227 ) ;
#91866=EDGE_LOOP ( 'NONE', ( #1997, #141312, #70687, #124693 ) ) ;
#91867=EDGE_LOOP ( 'NONE', ( #137580, #48119, #82581, #102858, #118321 ) ) ;
#91868=EDGE_LOOP ( 'NONE', ( #9167, #128467, #58769, #118988 ) ) ;
#91869=VECTOR ( 'NONE', #114997, 1000.000000000000000 ) ;
#91871=ORIENTED_EDGE ( 'NONE', *, *, #127720, .F. ) ;
#91872=DIRECTION ( 'NONE',  ( 0.000000000000000000, 0.000000000000000000, 1.000000000000000000 ) ) ;
#91873=AXIS2_PLACEMENT_3D ( 'NONE', #57142, #135409, #46266 ) ;
#91874=LINE ( 'NONE', #70870, #101215 ) ;
#91875=LINE ( 'NONE', #72322, #13306 ) ;
#91877=LINE ( 'NONE', #81029, #124155 ) ;
#91879=DIRECTION ( 'NONE',  ( 0.7071067811865486830, -0.7071067811865464625, -0.000000000000000000 ) ) ;
#91880=LINE ( 'NONE', #111494, #95250 ) ;
#91881=DIRECTION ( 'NONE',  ( 0.7071067811865486830, -0.7071067811865464625, -0.000000000000000000 ) ) ;
#91884=EDGE_CURVE ( 'NONE', #30305, #122724, #79484, .T. ) ;
#91885=CARTESIAN_POINT ( 'NONE',  ( -3.489213562373097322, -27.52281430457057709, 5.000000000000000000 ) ) ;
#91887=LINE ( 'NONE', #89749, #86340 ) ;
#91888=ORIENTED_EDGE ( 'NONE', *, *, #5928, .T. ) ;
#91889=ORIENTED_EDGE ( 'NONE', *, *, #90982, .T. ) ;
#91890=EDGE_CURVE ( 'NONE', #89147, #57984, #13421, .T. ) ;
#91891=CARTESIAN_POINT ( 'NONE',  ( -29.99451991528749417, 28.92564299267958816, 4.000000000000000000 ) ) ;
#91893=LINE ( 'NONE', #57883, #142658 ) ;
#91894=CARTESIAN_POINT ( 'NONE',  ( 14.99451991528749595, 28.92564299267948513, 4.000000000000000000 ) ) ;
#91897=DIRECTION ( 'NONE',  ( -0.7071067811865486830, -0.7071067811865464625, 0.000000000000000000 ) ) ;
#91898=CARTESIAN_POINT ( 'NONE',  ( -51.18398860626899705, 28.73617430169823095, 5.000000000000000000 ) ) ;
#91900=VECTOR ( 'NONE', #82147, 1000.000000000000000 ) ;
#91901=VERTEX_POINT ( 'NONE', #1809 ) ;
#91902=VERTEX_POINT ( 'NONE', #133123 ) ;
#91903=CARTESIAN_POINT ( 'NONE',  ( -15.48921356237309510, -27.52281430457066236, 5.000000000000000000 ) ) ;
#91904=VERTEX_POINT ( 'NONE', #67885 ) ;
#91905=VECTOR ( 'NONE', #57155, 1000.000000000000000 ) ;
#91906=EDGE_CURVE ( 'NONE', #75984, #19139, #91722, .T. ) ;
#91907=( BOUNDED_CURVE ( )  B_SPLINE_CURVE ( 3, ( #24325, #33109, #134537, #56291 ),
 .UNSPECIFIED., .F., .F. ) 
 B_SPLINE_CURVE_WITH_KNOTS ( ( 4, 4 ),
 ( 2.779374508378135378, 4.199602562396851368 ),
 .UNSPECIFIED. ) 
 CURVE ( )  GEOMETRIC_REPRESENTATION_ITEM ( )  RATIONAL_B_SPLINE_CURVE ( ( 1.000000000000000000, 0.8388583629366601624, 0.8388583629366601624, 1.000000000000000000 ) ) 
 REPRESENTATION_ITEM ( '' )  );
#91909=VERTEX_POINT ( 'NONE', #46111 ) ;
#91910=LINE ( 'NONE', #89765, #140881 ) ;
#91911=CARTESIAN_POINT ( 'NONE',  ( -30.32816939922332367, -21.74070752338405654, 4.000000000000000000 ) ) ;
#91912=LINE ( 'NONE', #46320, #29507 ) ;
#91913=VECTOR ( 'NONE', #106606, 1000.000000000000000 ) ;
#91916=FACE_OUTER_BOUND ( 'NONE', #89733, .T. ) ;
#91917=ORIENTED_EDGE ( 'NONE', *, *, #66006, .T. ) ;
#91919=FACE_OUTER_BOUND ( 'NONE', #115890, .T. ) ;
#91920=VERTEX_POINT ( 'NONE', #122193 ) ;
#91921=LINE ( 'NONE', #55754, #17938 ) ;
#91922=ORIENTED_EDGE ( 'NONE', *, *, #73753, .T. ) ;
#91923=ORIENTED_EDGE ( 'NONE', *, *, #70723, .F. ) ;
#91924=DIRECTION ( 'NONE',  ( -0.7071067811865486830, -0.7071067811865464625, 0.000000000000000000 ) ) ;
#91925=ORIENTED_EDGE ( 'NONE', *, *, #96843, .F. ) ;
#91926=ORIENTED_EDGE ( 'NONE', *, *, #91433, .F. ) ;
#91927=DIRECTION ( 'NONE',  ( 0.7071067811865487940, 0.7071067811865463515, -0.000000000000000000 ) ) ;
#91929=CARTESIAN_POINT ( 'NONE',  ( 23.99999999999983302, -0.1606350220012988939, 4.664761815935144718 ) ) ;
#91930=EDGE_CURVE ( 'NONE', #71270, #83728, #3273, .T. ) ;
#91931=FACE_OUTER_BOUND ( 'NONE', #82947, .T. ) ;
#91934=DIRECTION ( 'NONE',  ( -0.6830127018922180770, -0.6830127018922204085, -0.2588190451025213501 ) ) ;
#91936=DIRECTION ( 'NONE',  ( -0.6830127018922181881, 0.6830127018922202975, -0.2588190451025214056 ) ) ;
#91937=CARTESIAN_POINT ( 'NONE',  ( 51.48921356237309510, -27.52281430457091460, 5.000000000000000000 ) ) ;
#91938=DIRECTION ( 'NONE',  ( -0.7071067811865486830, -0.7071067811865464625, 0.000000000000000000 ) ) ;
#91939=FACE_OUTER_BOUND ( 'NONE', #44661, .T. ) ;
#91941=EDGE_CURVE ( 'NONE', #74437, #6107, #123676, .T. ) ;
#91943=DIRECTION ( 'NONE',  ( -0.3543493200069163240, 0.000000000000000000, -0.9351131265310288487 ) ) ;
#91944=ORIENTED_EDGE ( 'NONE', *, *, #41276, .F. ) ;
#91946=DIRECTION ( 'NONE',  ( 0.6830127018922180770, -0.6830127018922204085, -0.2588190451025213501 ) ) ;
#91947=ORIENTED_EDGE ( 'NONE', *, *, #82014, .T. ) ;
#91948=VERTEX_POINT ( 'NONE', #100479 ) ;
#91949=LINE ( 'NONE', #58681, #63463 ) ;
#91950=ORIENTED_EDGE ( 'NONE', *, *, #73588, .F. ) ;
#91951=LINE ( 'NONE', #60807, #113911 ) ;
#91953=CARTESIAN_POINT ( 'NONE',  ( -14.99999999999989519, 14.87792677143807651, -11.06722581663443350 ) ) ;
#91955=EDGE_CURVE ( 'NONE', #96580, #1511, #80873, .T. ) ;
#91956=CARTESIAN_POINT ( 'NONE',  ( 19.05000000000000071, 3.174999999999997158, 4.000000000000000000 ) ) ;
#91957=EDGE_CURVE ( 'NONE', #26241, #89121, #33801, .T. ) ;
#91958=DIRECTION ( 'NONE',  ( -0.7071067811865487940, 0.7071067811865463515, -0.000000000000000000 ) ) ;
#91960=LINE ( 'NONE', #115820, #51154 ) ;
#91962=AXIS2_PLACEMENT_3D ( 'NONE', #103992, #6093, #137384 ) ;
#91963=VECTOR ( 'NONE', #106874, 1000.000000000000227 ) ;
#91964=DIRECTION ( 'NONE',  ( -0.7071067811865487940, 0.7071067811865463515, -0.000000000000000000 ) ) ;
#91965=AXIS2_PLACEMENT_3D ( 'NONE', #106643, #7333, #51597 ) ;
#91967=EDGE_CURVE ( 'NONE', #54589, #19758, #101888, .T. ) ;
#91968=CARTESIAN_POINT ( 'NONE',  ( -9.489213562373095101, -27.52281430457062328, 5.000000000000000000 ) ) ;
#91969=CARTESIAN_POINT ( 'NONE',  ( -24.29974487139158867, -27.71228299555223273, 4.000000000000000000 ) ) ;
#91970=ORIENTED_EDGE ( 'NONE', *, *, #16156, .F. ) ;
#91971=ORIENTED_EDGE ( 'NONE', *, *, #133253, .T. ) ;
#91972=ORIENTED_EDGE ( 'NONE', *, *, #141252, .F. ) ;
#91973=LINE ( 'NONE', #123919, #5575 ) ;
#91974=LINE ( 'NONE', #38323, #90393 ) ;
#91975=VECTOR ( 'NONE', #90272, 1000.000000000000000 ) ;
#91976=EDGE_CURVE ( 'NONE', #98989, #59733, #1127, .T. ) ;
#91977=LINE ( 'NONE', #136194, #114531 ) ;
#91978=LINE ( 'NONE', #126728, #98293 ) ;
#91979=ORIENTED_EDGE ( 'NONE', *, *, #16269, .F. ) ;
#91980=DIRECTION ( 'NONE',  ( 0.7071067811865487940, -0.7071067811865463515, 0.000000000000000000 ) ) ;
#91982=DIRECTION ( 'NONE',  ( -0.7071067811865486830, -0.7071067811865464625, -0.000000000000000000 ) ) ;
#91983=DIRECTION ( 'NONE',  ( 0.7071067811865487940, 0.7071067811865463515, -0.000000000000000000 ) ) ;
#91984=ORIENTED_EDGE ( 'NONE', *, *, #103513, .F. ) ;
#91985=EDGE_CURVE ( 'NONE', #23205, #131546, #14156, .T. ) ;
#91986=CARTESIAN_POINT ( 'NONE',  ( -32.99451991528749062, 28.92564299267960948, 4.000000000000000000 ) ) ;
#91987=VERTEX_POINT ( 'NONE', #80169 ) ;
#91989=VERTEX_POINT ( 'NONE', #124359 ) ;
#91990=EDGE_LOOP ( 'NONE', ( #13379, #72993, #108945, #97628 ) ) ;
#91992=DIRECTION ( 'NONE',  ( -0.7071067811865486830, 0.7071067811865464625, 0.000000000000000000 ) ) ;
#91993=VECTOR ( 'NONE', #46734, 1000.000000000000227 ) ;
#91994=EDGE_CURVE ( 'NONE', #25602, #20468, #58446, .T. ) ;
#91995=ORIENTED_EDGE ( 'NONE', *, *, #116883, .F. ) ;
#91996=CARTESIAN_POINT ( 'NONE',  ( -5.999999999999946709, -19.44781430457062754, 5.000000000000000000 ) ) ;
#91997=FACE_OUTER_BOUND ( 'NONE', #38895, .T. ) ;
#91998=DIRECTION ( 'NONE',  ( -0.000000000000000000, 0.3543493200069153248, 0.9351131265310292928 ) ) ;
#92001=VECTOR ( 'NONE', #86831, 1000.000000000000000 ) ;
#92002=FACE_OUTER_BOUND ( 'NONE', #73492, .T. ) ;
#92005=DIRECTION ( 'NONE',  ( -0.7071067811865487940, 0.7071067811865463515, 0.000000000000000000 ) ) ;
#92006=CARTESIAN_POINT ( 'NONE',  ( -33.18398860626899705, 28.73617430169810305, 5.000000000000000000 ) ) ;
#92007=LINE ( 'NONE', #56589, #39131 ) ;
#92010=VECTOR ( 'NONE', #30928, 1000.000000000000227 ) ;
#92011=CARTESIAN_POINT ( 'NONE',  ( 26.99999999999981881, -4.447814304570781196, 5.000000000000000000 ) ) ;
#92012=CARTESIAN_POINT ( 'NONE',  ( 5.999999999999958256, 15.45873954670186201, -0.03131636524295391966 ) ) ;
#92013=CARTESIAN_POINT ( 'NONE',  ( 29.29289321881325137, 5.259292476615669010, 5.000000000000000000 ) ) ;
#92015=ORIENTED_EDGE ( 'NONE', *, *, #55572, .F. ) ;
#92017=VERTEX_POINT ( 'NONE', #93157 ) ;
#92018=VERTEX_POINT ( 'NONE', #70021 ) ;
#92019=AXIS2_PLACEMENT_3D ( 'NONE', #74024, #131255, #109500 ) ;
#92021=DIRECTION ( 'NONE',  ( 0.7071067811865487940, -0.7071067811865463515, 0.000000000000000000 ) ) ;
#92022=CARTESIAN_POINT ( 'NONE',  ( -23.29289321881329755, -12.74070752338414891, 5.000000000000000000 ) ) ;
#92023=ORIENTED_EDGE ( 'NONE', *, *, #4292, .F. ) ;
#92024=CARTESIAN_POINT ( 'NONE',  ( 0.000000000000000000, 0.000000000000000000, 5.000000000000000000 ) ) ;
#92026=DIRECTION ( 'NONE',  ( -0.6830127018922181881, 0.6830127018922202975, -0.2588190451025214056 ) ) ;
#92029=LINE ( 'NONE', #60889, #102935 ) ;
#92030=DIRECTION ( 'NONE',  ( 0.7071067811865487940, 0.7071067811865463515, 0.000000000000000000 ) ) ;
#92031=LINE ( 'NONE', #136254, #130325 ) ;
#92032=LINE ( 'NONE', #67474, #100981 ) ;
#92033=LINE ( 'NONE', #136257, #98497 ) ;
#92035=ORIENTED_EDGE ( 'NONE', *, *, #65172, .F. ) ;
#92039=ORIENTED_EDGE ( 'NONE', *, *, #17750, .F. ) ;
#92040=PLANE ( 'NONE',  #121899 ) ;
#92042=ORIENTED_EDGE ( 'NONE', *, *, #26546, .F. ) ;
#92043=CARTESIAN_POINT ( 'NONE',  ( 28.49999999999980815, -17.56887692260762535, 4.000000000000000000 ) ) ;
#92046=EDGE_LOOP ( 'NONE', ( #127595, #20806, #126024, #74223 ) ) ;
#92047=VERTEX_POINT ( 'NONE', #95290 ) ;
#92049=CARTESIAN_POINT ( 'NONE',  ( 0.000000000000000000, 0.000000000000000000, 5.000000000000000000 ) ) ;
#92050=VECTOR ( 'NONE', #121543, 1000.000000000000000 ) ;
#92051=EDGE_LOOP ( 'NONE', ( #47736, #141256, #20216 ) ) ;
#92052=ORIENTED_EDGE ( 'NONE', *, *, #84429, .T. ) ;
#92053=VECTOR ( 'NONE', #111328, 1000.000000000000227 ) ;
#92054=EDGE_CURVE ( 'NONE', #73062, #23978, #50376, .T. ) ;
#92055=ORIENTED_EDGE ( 'NONE', *, *, #139906, .F. ) ;
#92056=DIRECTION ( 'NONE',  ( -0.000000000000000000, -0.3543493200069152693, 0.9351131265310292928 ) ) ;
#92058=ADVANCED_FACE ( 'NONE', ( #126481 ), #117040, .F. ) ;
#92060=AXIS2_PLACEMENT_3D ( 'NONE', #108733, #29764, #41359 ) ;
#92063=EDGE_LOOP ( 'NONE', ( #74462, #65158, #64251, #55328 ) ) ;
#92065=VERTEX_POINT ( 'NONE', #51096 ) ;
#92066=CARTESIAN_POINT ( 'NONE',  ( 5.999999999999965361, -9.033600742197647193, 5.000000000000000000 ) ) ;
#92067=ORIENTED_EDGE ( 'NONE', *, *, #8309, .T. ) ;
#92068=ORIENTED_EDGE ( 'NONE', *, *, #50166, .T. ) ;
#92069=LINE ( 'NONE', #124714, #139712 ) ;
#92070=EDGE_CURVE ( 'NONE', #46120, #59760, #61980, .T. ) ;
#92071=DIRECTION ( 'NONE',  ( -0.7071067811865487940, 0.7071067811865463515, 0.000000000000000000 ) ) ;
#92072=ORIENTED_EDGE ( 'NONE', *, *, #23343, .T. ) ;
#92073=CARTESIAN_POINT ( 'NONE',  ( 0.000000000000000000, 0.000000000000000000, 5.000000000000000000 ) ) ;
#92074=CARTESIAN_POINT ( 'NONE',  ( -29.29289321881324426, 8.259292476615632594, 5.000000000000000000 ) ) ;
#92075=LINE ( 'NONE', #15908, #129406 ) ;
#92076=ADVANCED_FACE ( 'NONE', ( #49684 ), #6812, .T. ) ;
#92077=CARTESIAN_POINT ( 'NONE',  ( 60.48921356237309510, -27.52281430457097500, 5.000000000000000000 ) ) ;
#92078=FACE_BOUND ( 'NONE', #36721, .T. ) ;
#92079=ORIENTED_EDGE ( 'NONE', *, *, #139089, .F. ) ;
#92080=DIRECTION ( 'NONE',  ( 0.7071067811865486830, -0.7071067811865464625, -0.000000000000000000 ) ) ;
#92083=ORIENTED_EDGE ( 'NONE', *, *, #43085, .F. ) ;
#92084=LINE ( 'NONE', #91408, #143090 ) ;
#92085=ORIENTED_EDGE ( 'NONE', *, *, #72711, .F. ) ;
#92086=VECTOR ( 'NONE', #120245, 1000.000000000000000 ) ;
#92087=ADVANCED_FACE ( 'NONE', ( #48222 ), #136650, .F. ) ;
#92090=EDGE_LOOP ( 'NONE', ( #66603, #117242, #140616, #132842 ) ) ;
#92093=PLANE ( 'NONE',  #81133 ) ;
#92094=DIRECTION ( 'NONE',  ( 0.3543493200069162685, -0.000000000000000000, -0.9351131265310288487 ) ) ;
#92095=CARTESIAN_POINT ( 'NONE',  ( -26.29289321881326913, -15.74070752338412049, 5.000000000000000000 ) ) ;
#92096=ADVANCED_FACE ( 'NONE', ( #59832 ), #59147, .T. ) ;
#92098=CARTESIAN_POINT ( 'NONE',  ( 34.49999999999975131, -2.568876922607791879, 4.000000000000000000 ) ) ;
#92099=PLANE ( 'NONE',  #42215 ) ;
#92100=ADVANCED_FACE ( 'NONE', ( #127199 ), #38080, .F. ) ;
#92101=EDGE_CURVE ( 'NONE', #21299, #17453, #137388, .T. ) ;
#92102=FACE_OUTER_BOUND ( 'NONE', #124454, .T. ) ;
#92105=FACE_OUTER_BOUND ( 'NONE', #104307, .T. ) ;
#92106=ORIENTED_EDGE ( 'NONE', *, *, #16948, .F. ) ;
#92107=ORIENTED_EDGE ( 'NONE', *, *, #24460, .T. ) ;
#92108=VERTEX_POINT ( 'NONE', #70726 ) ;
#92109=ORIENTED_EDGE ( 'NONE', *, *, #110774, .F. ) ;
#92110=LINE ( 'NONE', #136337, #17069 ) ;
#92111=ORIENTED_EDGE ( 'NONE', *, *, #28610, .F. ) ;
#92112=EDGE_CURVE ( 'NONE', #89225, #79591, #71418, .T. ) ;
#92113=ORIENTED_EDGE ( 'NONE', *, *, #58594, .T. ) ;
#92116=ADVANCED_FACE ( 'NONE', ( #19865 ), #119179, .F. ) ;
#92117=CARTESIAN_POINT ( 'NONE',  ( 0.005480084712502889671, 28.92564299267938210, 4.000000000000000000 ) ) ;
#92118=VERTEX_POINT ( 'NONE', #74273 ) ;
#92119=CARTESIAN_POINT ( 'NONE',  ( 16.49999999999988631, 12.05218569542904561, 5.000000000000000000 ) ) ;
#92120=VERTEX_POINT ( 'NONE', #40926 ) ;
#92121=CARTESIAN_POINT ( 'NONE',  ( 0.000000000000000000, 0.000000000000000000, 5.000000000000000000 ) ) ;
#92122=CARTESIAN_POINT ( 'NONE',  ( 33.18398860626899705, 28.73617430169810305, 5.000000000000000000 ) ) ;
#92124=ORIENTED_EDGE ( 'NONE', *, *, #14160, .T. ) ;
#92126=CARTESIAN_POINT ( 'NONE',  ( 34.42499999999998295, 0.000000000000000000, 4.500000000000000888 ) ) ;
#92127=EDGE_CURVE ( 'NONE', #122527, #139318, #20573, .T. ) ;
#92128=LINE ( 'NONE', #113166, #81319 ) ;
#92131=ORIENTED_EDGE ( 'NONE', *, *, #52527, .T. ) ;
#92133=ORIENTED_EDGE ( 'NONE', *, *, #18392, .F. ) ;
#92134=DIRECTION ( 'NONE',  ( -0.6830127018922181881, 0.6830127018922202975, -0.2588190451025214056 ) ) ;
#92135=DIRECTION ( 'NONE',  ( 0.7071067811865487940, -0.7071067811865463515, 0.000000000000000000 ) ) ;
#92136=ADVANCED_FACE ( 'NONE', ( #41623 ), #53966, .F. ) ;
#92137=LINE ( 'NONE', #58147, #19182 ) ;
#92138=ORIENTED_EDGE ( 'NONE', *, *, #32006, .T. ) ;
#92139=DIRECTION ( 'NONE',  ( -0.7071067811865486830, 0.7071067811865464625, 0.000000000000000000 ) ) ;
#92140=VECTOR ( 'NONE', #130748, 1000.000000000000000 ) ;
#92142=DIRECTION ( 'NONE',  ( -0.7071067811865487940, 0.7071067811865463515, 0.000000000000000000 ) ) ;
#92143=VERTEX_POINT ( 'NONE', #8249 ) ;
#92144=DIRECTION ( 'NONE',  ( -0.000000000000000000, 0.000000000000000000, 1.000000000000000000 ) ) ;
#92145=LINE ( 'NONE', #135682, #2918 ) ;
#92146=ORIENTED_EDGE ( 'NONE', *, *, #33033, .T. ) ;
#92147=VECTOR ( 'NONE', #86586, 1000.000000000000000 ) ;
#92148=DIRECTION ( 'NONE',  ( 0.7071067811865487940, 0.7071067811865463515, -0.000000000000000000 ) ) ;
#92149=ORIENTED_EDGE ( 'NONE', *, *, #20533, .F. ) ;
#92150=EDGE_LOOP ( 'NONE', ( #141752, #88570, #29414, #132691 ) ) ;
#92151=LINE ( 'NONE', #37072, #49389 ) ;
#92152=CARTESIAN_POINT ( 'NONE',  ( -14.99999999999990230, -16.02097659208072855, -11.96015758381205707 ) ) ;
#92153=VECTOR ( 'NONE', #15407, 1000.000000000000000 ) ;
#92154=VERTEX_POINT ( 'NONE', #18411 ) ;
#92156=AXIS2_PLACEMENT_3D ( 'NONE', #111539, #10772, #55040 ) ;
#92158=LINE ( 'NONE', #16754, #38261 ) ;
#92159=EDGE_CURVE ( 'NONE', #19533, #119254, #120588, .T. ) ;
#92160=DIRECTION ( 'NONE',  ( -0.3543493200069162685, -0.000000000000000000, -0.9351131265310288487 ) ) ;
#92161=VERTEX_POINT ( 'NONE', #129341 ) ;
#92162=CARTESIAN_POINT ( 'NONE',  ( -14.27718569542929572, -21.72500000000000142, 5.000000000000000000 ) ) ;
#92164=LINE ( 'NONE', #27627, #42039 ) ;
#92165=LINE ( 'NONE', #4389, #28592 ) ;
#92167=EDGE_CURVE ( 'NONE', #68527, #22961, #31478, .T. ) ;
#92168=FACE_OUTER_BOUND ( 'NONE', #70214, .T. ) ;
#92169=CARTESIAN_POINT ( 'NONE',  ( -42.29974487139158157, -27.71228299555235708, 4.000000000000000000 ) ) ;
#92170=ORIENTED_EDGE ( 'NONE', *, *, #93622, .T. ) ;
#92171=ORIENTED_EDGE ( 'NONE', *, *, #46314, .T. ) ;
#92172=ORIENTED_EDGE ( 'NONE', *, *, #11226, .T. ) ;
#92174=VERTEX_POINT ( 'NONE', #65569 ) ;
#92175=ORIENTED_EDGE ( 'NONE', *, *, #81387, .T. ) ;
#92176=ORIENTED_EDGE ( 'NONE', *, *, #7924, .F. ) ;
#92178=VECTOR ( 'NONE', #124644, 999.9999999999998863 ) ;
#92180=ORIENTED_EDGE ( 'NONE', *, *, #84266, .T. ) ;
#92181=CARTESIAN_POINT ( 'NONE',  ( -13.49999999999990408, 21.43112307739196609, 4.000000000000000000 ) ) ;
#92182=VECTOR ( 'NONE', #44612, 1000.000000000000000 ) ;
#92183=FACE_OUTER_BOUND ( 'NONE', #18064, .T. ) ;
#92184=DIRECTION ( 'NONE',  ( 0.6830127018922180770, -0.6830127018922204085, -0.2588190451025213501 ) ) ;
#92186=ORIENTED_EDGE ( 'NONE', *, *, #58232, .T. ) ;
#92187=DIRECTION ( 'NONE',  ( -0.7071067811865486830, -0.7071067811865464625, 0.000000000000000000 ) ) ;
#92188=DIRECTION ( 'NONE',  ( 0.7071067811865487940, 0.7071067811865463515, -0.000000000000000000 ) ) ;
#92189=VECTOR ( 'NONE', #55054, 1000.000000000000000 ) ;
#92190=LINE ( 'NONE', #58210, #123741 ) ;
#92192=CARTESIAN_POINT ( 'NONE',  ( 17.99999999999987566, -9.033600742197641864, 5.000000000000000000 ) ) ;
#92193=CARTESIAN_POINT ( 'NONE',  ( -29.99451991528749417, 28.92564299267958816, 4.000000000000000000 ) ) ;
#92194=DIRECTION ( 'NONE',  ( -0.7071067811865487940, 0.7071067811865463515, 0.000000000000000000 ) ) ;
#92196=CARTESIAN_POINT ( 'NONE',  ( 41.99451991528749062, 28.92564299267967343, 4.000000000000000000 ) ) ;
#92198=VERTEX_POINT ( 'NONE', #143085 ) ;
#92201=ORIENTED_EDGE ( 'NONE', *, *, #77749, .F. ) ;
#92202=VERTEX_POINT ( 'NONE', #8942 ) ;
#92203=DIRECTION ( 'NONE',  ( 0.7071067811865487940, 0.7071067811865463515, -0.000000000000000000 ) ) ;
#92204=ADVANCED_FACE ( 'NONE', ( #75700 ), #53206, .T. ) ;
#92206=ORIENTED_EDGE ( 'NONE', *, *, #124245, .F. ) ;
#92207=AXIS2_PLACEMENT_3D ( 'NONE', #70931, #68797, #62732 ) ;
#92208=LINE ( 'NONE', #69806, #94132 ) ;
#92209=PLANE ( 'NONE',  #63100 ) ;
#92213=ORIENTED_EDGE ( 'NONE', *, *, #111397, .F. ) ;
#92214=CARTESIAN_POINT ( 'NONE',  ( -12.48921356237309155, -27.52281430457064104, 5.000000000000000000 ) ) ;
#92215=ORIENTED_EDGE ( 'NONE', *, *, #138182, .F. ) ;
#92216=CARTESIAN_POINT ( 'NONE',  ( -10.49999999999992539, 22.22500000000000853, 4.362957392718823435 ) ) ;
#92217=CARTESIAN_POINT ( 'NONE',  ( -29.99451991528749417, 28.92564299267958816, 4.000000000000000000 ) ) ;
#92219=EDGE_CURVE ( 'NONE', #36583, #36166, #97414, .T. ) ;
#92220=CARTESIAN_POINT ( 'NONE',  ( 2.999999999999981792, -1.068876922607802538, 4.000000000000000000 ) ) ;
#92221=ORIENTED_EDGE ( 'NONE', *, *, #112248, .F. ) ;
#92222=EDGE_CURVE ( 'NONE', #25213, #26153, #27053, .T. ) ;
#92224=EDGE_LOOP ( 'NONE', ( #8165, #112459, #59203, #91075 ) ) ;
#92226=CARTESIAN_POINT ( 'NONE',  ( 0.000000000000000000, 0.000000000000000000, 5.000000000000000000 ) ) ;
#92228=DIRECTION ( 'NONE',  ( -0.000000000000000000, 0.3543493200069153248, 0.9351131265310292928 ) ) ;
#92229=EDGE_CURVE ( 'NONE', #98543, #66493, #87285, .T. ) ;
#92230=ADVANCED_FACE ( 'NONE', ( #95996 ), #99555, .F. ) ;
#92232=CARTESIAN_POINT ( 'NONE',  ( -24.29974487139158867, -27.71228299555223273, 4.000000000000000000 ) ) ;
#92233=EDGE_CURVE ( 'NONE', #115804, #92397, #58275, .T. ) ;
#92234=CARTESIAN_POINT ( 'NONE',  ( 32.99999999999977263, -6.108550654416931458, -3.114665004254893343 ) ) ;
#92235=ORIENTED_EDGE ( 'NONE', *, *, #16315, .T. ) ;
#92236=EDGE_LOOP ( 'NONE', ( #114504, #43337, #7360, #64901 ) ) ;
#92237=DIRECTION ( 'NONE',  ( 0.7071067811865486830, -0.7071067811865464625, -0.000000000000000000 ) ) ;
#92238=ORIENTED_EDGE ( 'NONE', *, *, #76601, .F. ) ;
#92239=EDGE_CURVE ( 'NONE', #103031, #116321, #23437, .T. ) ;
#92241=ORIENTED_EDGE ( 'NONE', *, *, #53551, .T. ) ;
#92242=CARTESIAN_POINT ( 'NONE',  ( 9.183988606268997046, 28.73617430169793607, 5.000000000000000000 ) ) ;
#92243=AXIS2_PLACEMENT_3D ( 'NONE', #116526, #25953, #37556 ) ;
#92244=EDGE_CURVE ( 'NONE', #31004, #115675, #57530, .T. ) ;
#92245=VECTOR ( 'NONE', #114765, 1000.000000000000000 ) ;
#92246=VECTOR ( 'NONE', #8763, 1000.000000000000000 ) ;
#92249=FACE_BOUND ( 'NONE', #136890, .T. ) ;
#92250=DIRECTION ( 'NONE',  ( 0.6830127018922181881, 0.6830127018922202975, -0.2588190451025214056 ) ) ;
#92251=CARTESIAN_POINT ( 'NONE',  ( 23.70025512860841133, -27.71228299555189523, 4.000000000000000000 ) ) ;
#92252=CARTESIAN_POINT ( 'NONE',  ( 21.70710678118639692, 11.25929247661560417, 5.000000000000000000 ) ) ;
#92254=LINE ( 'NONE', #35793, #62082 ) ;
#92255=EDGE_LOOP ( 'NONE', ( #49847, #13114, #15644, #31266 ) ) ;
#92256=EDGE_CURVE ( 'NONE', #98989, #44722, #124187, .T. ) ;
#92257=VECTOR ( 'NONE', #110990, 1000.000000000000000 ) ;
#92258=AXIS2_PLACEMENT_3D ( 'NONE', #69985, #138053, #114148 ) ;
#92260=VERTEX_POINT ( 'NONE', #957 ) ;
#92261=ORIENTED_EDGE ( 'NONE', *, *, #51160, .F. ) ;
#92263=ORIENTED_EDGE ( 'NONE', *, *, #122102, .T. ) ;
#92264=DIRECTION ( 'NONE',  ( -0.6830127018922181881, 0.6830127018922202975, -0.2588190451025214056 ) ) ;
#92265=EDGE_CURVE ( 'NONE', #99187, #64475, #132240, .T. ) ;
#92266=ORIENTED_EDGE ( 'NONE', *, *, #141566, .F. ) ;
#92267=CARTESIAN_POINT ( 'NONE',  ( 32.20710678118632586, -20.24070752338407075, 5.000000000000000000 ) ) ;
#92269=DIRECTION ( 'NONE',  ( -0.7071067811865486830, 0.7071067811865464625, 0.000000000000000000 ) ) ;
#92270=EDGE_CURVE ( 'NONE', #71223, #61774, #11833, .T. ) ;
#92271=AXIS2_PLACEMENT_3D ( 'NONE', #127893, #27839, #28574 ) ;
#92273=CARTESIAN_POINT ( 'NONE',  ( -63.48921356237309510, -27.52281430457099631, 5.000000000000000000 ) ) ;
#92274=EDGE_CURVE ( 'NONE', #55534, #4302, #12557, .T. ) ;
#92276=PLANE ( 'NONE',  #20747 ) ;
#92278=AXIS2_PLACEMENT_3D ( 'NONE', #111636, #45695, #102197 ) ;
#92279=ORIENTED_EDGE ( 'NONE', *, *, #100564, .F. ) ;
#92281=DIRECTION ( 'NONE',  ( 1.000000000000000000, 0.000000000000000000, 0.000000000000000000 ) ) ;
#92282=ORIENTED_EDGE ( 'NONE', *, *, #48782, .T. ) ;
#92284=EDGE_CURVE ( 'NONE', #81393, #64729, #46690, .T. ) ;
#92285=ORIENTED_EDGE ( 'NONE', *, *, #80394, .T. ) ;
#92286=VERTEX_POINT ( 'NONE', #100997 ) ;
#92287=DIRECTION ( 'NONE',  ( 0.6830127018922180770, -0.6830127018922204085, -0.2588190451025213501 ) ) ;
#92288=ORIENTED_EDGE ( 'NONE', *, *, #42325, .T. ) ;
#92289=VECTOR ( 'NONE', #65298, 1000.000000000000000 ) ;
#92290=CARTESIAN_POINT ( 'NONE',  ( -16.82816939922340893, -20.24070752338407431, 4.000000000000000000 ) ) ;
#92294=CARTESIAN_POINT ( 'NONE',  ( -18.48921356237309510, -27.52281430457068367, 5.000000000000000000 ) ) ;
#92295=VERTEX_POINT ( 'NONE', #2368 ) ;
#92296=EDGE_CURVE ( 'NONE', #68931, #34970, #60199, .T. ) ;
#92297=DIRECTION ( 'NONE',  ( -0.7071067811865486830, -0.7071067811865464625, 0.000000000000000000 ) ) ;
#92299=VECTOR ( 'NONE', #133717, 1000.000000000000000 ) ;
#92300=DIRECTION ( 'NONE',  ( -0.000000000000000000, 0.3543493200069152138, -0.9351131265310292928 ) ) ;
#92301=ORIENTED_EDGE ( 'NONE', *, *, #121237, .F. ) ;
#92303=LINE ( 'NONE', #81483, #54256 ) ;
#92304=LINE ( 'NONE', #71308, #23745 ) ;
#92305=CARTESIAN_POINT ( 'NONE',  ( 11.99999999999991296, -16.02097659208071079, -11.96015758381211569 ) ) ;
#92306=ORIENTED_EDGE ( 'NONE', *, *, #14963, .F. ) ;
#92307=LINE ( 'NONE', #136530, #92245 ) ;
#92309=CARTESIAN_POINT ( 'NONE',  ( 34.92499999999998295, -19.29806943317882784, 4.500000000000000888 ) ) ;
#92310=CARTESIAN_POINT ( 'NONE',  ( -14.99999999999989875, 10.93112307739207623, 4.000000000000000000 ) ) ;
#92311=LINE ( 'NONE', #93765, #14295 ) ;
#92312=ORIENTED_EDGE ( 'NONE', *, *, #97429, .T. ) ;
#92313=CARTESIAN_POINT ( 'NONE',  ( -3.489213562373097322, -27.52281430457057709, 5.000000000000000000 ) ) ;
#92314=CARTESIAN_POINT ( 'NONE',  ( 34.92499999999998295, 12.66246187583888450, 4.000000000000000000 ) ) ;
#92316=LINE ( 'NONE', #35862, #79514 ) ;
#92317=ADVANCED_FACE ( 'NONE', ( #11103 ), #89416, .F. ) ;
#92319=VERTEX_POINT ( 'NONE', #78555 ) ;
#92320=VERTEX_POINT ( 'NONE', #111894 ) ;
#92321=CARTESIAN_POINT ( 'NONE',  ( 25.01899999999999835, 3.174999999999997158, 1.444000000000000394 ) ) ;
#92325=EDGE_CURVE ( 'NONE', #29884, #16488, #35069, .T. ) ;
#92326=CARTESIAN_POINT ( 'NONE',  ( 42.18398860626899705, 28.73617430169816700, 5.000000000000000000 ) ) ;
#92327=CARTESIAN_POINT ( 'NONE',  ( 15.48921356237309510, -27.52281430457066236, 5.000000000000000000 ) ) ;
#92328=CARTESIAN_POINT ( 'NONE',  ( -30.79289321881324071, -17.24070752338410628, 5.000000000000000000 ) ) ;
#92329=VERTEX_POINT ( 'NONE', #1653 ) ;
#92330=FACE_OUTER_BOUND ( 'NONE', #91866, .T. ) ;
#92331=DIRECTION ( 'NONE',  ( 0.7071067811865487940, 0.7071067811865463515, -0.000000000000000000 ) ) ;
#92334=EDGE_CURVE ( 'NONE', #142484, #5541, #45936, .T. ) ;
#92335=CARTESIAN_POINT ( 'NONE',  ( 39.48921356237310221, -27.52281430457082934, 5.000000000000000000 ) ) ;
#92336=ADVANCED_FACE ( 'NONE', ( #77152 ), #112602, .F. ) ;
#92338=PLANE ( 'NONE',  #81259 ) ;
#92339=ORIENTED_EDGE ( 'NONE', *, *, #11098, .T. ) ;
#92340=LINE ( 'NONE', #50830, #127070 ) ;
#92342=CARTESIAN_POINT ( 'NONE',  ( -47.99451991528749062, 28.92564299267971251, 4.000000000000000000 ) ) ;
#92343=AXIS2_PLACEMENT_3D ( 'NONE', #94585, #92432, #137405 ) ;
#92344=AXIS2_PLACEMENT_3D ( 'NONE', #18492, #38154, #51168 ) ;
#92346=DIRECTION ( 'NONE',  ( 0.7071067811865487940, 0.7071067811865463515, 0.000000000000000000 ) ) ;
#92347=DIRECTION ( 'NONE',  ( 0.6830127018922181881, 0.6830127018922202975, -0.2588190451025214056 ) ) ;
#92348=AXIS2_PLACEMENT_3D ( 'NONE', #110088, #88375, #132613 ) ;
#92349=CARTESIAN_POINT ( 'NONE',  ( 15.42327845806343944, 11.25929247661560240, 17.85071094206580966 ) ) ;
#92350=EDGE_CURVE ( 'NONE', #43579, #84626, #69111, .T. ) ;
#92351=DIRECTION ( 'NONE',  ( -0.6830127018922180770, -0.6830127018922204085, -0.2588190451025214056 ) ) ;
#92353=VERTEX_POINT ( 'NONE', #3110 ) ;
#92354=CARTESIAN_POINT ( 'NONE',  ( -9.781626882924873811, 21.74787736706806740, 4.999607392498049308 ) ) ;
#92355=CARTESIAN_POINT ( 'NONE',  ( -32.99451991528749062, 28.92564299267960948, 4.000000000000000000 ) ) ;
#92358=CARTESIAN_POINT ( 'NONE',  ( -5.241399257802002332, 21.72500000000000853, 5.000000000000000000 ) ) ;
#92361=CARTESIAN_POINT ( 'NONE',  ( 21.32816939922337696, -12.74070752338415424, 4.000000000000000000 ) ) ;
#92362=ORIENTED_EDGE ( 'NONE', *, *, #101720, .F. ) ;
#92363=VERTEX_POINT ( 'NONE', #32932 ) ;
#92365=LINE ( 'NONE', #102576, #102580 ) ;
#92366=CARTESIAN_POINT ( 'NONE',  ( -19.49999999999986500, -7.533600742197656963, 5.000000000000000000 ) ) ;
#92367=DIRECTION ( 'NONE',  ( -0.000000000000000000, 0.3543493200069153248, 0.9351131265310292928 ) ) ;
#92368=AXIS2_PLACEMENT_3D ( 'NONE', #88457, #79022, #123937 ) ;
#92370=CARTESIAN_POINT ( 'NONE',  ( 10.96659967656970736, 6.759292476615645917, 12.28218704918524828 ) ) ;
#92371=VECTOR ( 'NONE', #110375, 1000.000000000000000 ) ;
#92373=DIRECTION ( 'NONE',  ( 0.7071067811865487940, -0.7071067811865463515, 0.000000000000000000 ) ) ;
#92374=ORIENTED_EDGE ( 'NONE', *, *, #39764, .T. ) ;
#92375=VERTEX_POINT ( 'NONE', #71977 ) ;
#92377=VECTOR ( 'NONE', #83716, 1000.000000000000227 ) ;
#92378=AXIS2_PLACEMENT_3D ( 'NONE', #118567, #62797, #63522 ) ;
#92379=CARTESIAN_POINT ( 'NONE',  ( 19.49999999999987210, 10.08746187583914278, 4.000000000000000000 ) ) ;
#92381=AXIS2_PLACEMENT_3D ( 'NONE', #86832, #109989, #19416 ) ;
#92383=PLANE ( 'NONE',  #67366 ) ;
#92384=EDGE_CURVE ( 'NONE', #106219, #19553, #135781, .T. ) ;
#92385=EDGE_CURVE ( 'NONE', #107048, #125144, #115405, .T. ) ;
#92386=CARTESIAN_POINT ( 'NONE',  ( -17.99999999999986855, -19.44781430457062754, 5.000000000000000000 ) ) ;
#92387=EDGE_LOOP ( 'NONE', ( #16843, #91140, #68436, #98859 ) ) ;
#92388=CARTESIAN_POINT ( 'NONE',  ( -19.49999999999986500, -15.29013452822856145, 0.3645803511609898018 ) ) ;
#92389=LINE ( 'NONE', #4617, #45442 ) ;
#92390=CARTESIAN_POINT ( 'NONE',  ( -3.489213562373097322, -27.52281430457057709, 5.000000000000000000 ) ) ;
#92391=VECTOR ( 'NONE', #130930, 1000.000000000000000 ) ;
#92393=AXIS2_PLACEMENT_3D ( 'NONE', #134967, #109607, #101576 ) ;
#92394=EDGE_CURVE ( 'NONE', #133168, #143141, #38612, .T. ) ;
#92395=ORIENTED_EDGE ( 'NONE', *, *, #32028, .F. ) ;
#92397=VERTEX_POINT ( 'NONE', #25573 ) ;
#92398=EDGE_CURVE ( 'NONE', #13957, #80820, #103824, .T. ) ;
#92399=DIRECTION ( 'NONE',  ( 0.7071067811865486830, -0.7071067811865464625, -0.000000000000000000 ) ) ;
#92400=LINE ( 'NONE', #82286, #120460 ) ;
#92401=LINE ( 'NONE', #136628, #15497 ) ;
#92402=EDGE_CURVE ( 'NONE', #91522, #11791, #15384, .T. ) ;
#92403=PLANE ( 'NONE',  #77915 ) ;
#92405=ORIENTED_EDGE ( 'NONE', *, *, #49478, .T. ) ;
#92406=VERTEX_POINT ( 'NONE', #83560 ) ;
#92408=EDGE_CURVE ( 'NONE', #71767, #22720, #17546, .T. ) ;
#92409=CARTESIAN_POINT ( 'NONE',  ( -20.56494995367816614, -2.598550695876024275, 5.000000000000000000 ) ) ;
#92410=EDGE_CURVE ( 'NONE', #126070, #104812, #80704, .T. ) ;
#92411=ORIENTED_EDGE ( 'NONE', *, *, #91099, .F. ) ;
#92412=CARTESIAN_POINT ( 'NONE',  ( -21.52400138585434064, 22.03583458319437582, 4.979811245910087614 ) ) ;
#92413=EDGE_LOOP ( 'NONE', ( #95084, #107215, #75986, #70980 ) ) ;
#92414=CARTESIAN_POINT ( 'NONE',  ( -44.99451991528749772, 28.92564299267969474, 4.000000000000000000 ) ) ;
#92415=EDGE_CURVE ( 'NONE', #35605, #49913, #116873, .T. ) ;
#92416=FACE_BOUND ( 'NONE', #72197, .T. ) ;
#92417=CARTESIAN_POINT ( 'NONE',  ( 0.000000000000000000, 0.000000000000000000, 5.000000000000000000 ) ) ;
#92418=DIRECTION ( 'NONE',  ( 0.7071067811865487940, 0.7071067811865463515, 0.000000000000000000 ) ) ;
#92420=DIRECTION ( 'NONE',  ( 2.781805975412905890E-17, -0.3543493200069152693, 0.9351131265310292928 ) ) ;
#92422=LINE ( 'NONE', #58451, #122734 ) ;
#92424=ORIENTED_EDGE ( 'NONE', *, *, #22429, .F. ) ;
#92425=ORIENTED_EDGE ( 'NONE', *, *, #30413, .T. ) ;
#92427=VERTEX_POINT ( 'NONE', #127024 ) ;
#92428=DIRECTION ( 'NONE',  ( 0.6830127018922181881, 0.6830127018922202975, -0.2588190451025214056 ) ) ;
#92429=LINE ( 'NONE', #14887, #16640 ) ;
#92430=LINE ( 'NONE', #73574, #130500 ) ;
#92431=VERTEX_POINT ( 'NONE', #48067 ) ;
#92432=DIRECTION ( 'NONE',  ( -0.6830127018922180770, -0.6830127018922204085, -0.2588190451025213501 ) ) ;
#92433=CARTESIAN_POINT ( 'NONE',  ( 21.71757738642552127, -21.73023691814493574, 5.000000000000000888 ) ) ;
#92434=DIRECTION ( 'NONE',  ( 0.7071067811865487940, 0.7071067811865463515, 0.000000000000000000 ) ) ;
#92435=DIRECTION ( 'NONE',  ( 0.6830127018922181881, 0.6830127018922202975, -0.2588190451025214056 ) ) ;
#92437=CARTESIAN_POINT ( 'NONE',  ( 24.48921356237309510, -27.52281430457072631, 5.000000000000000000 ) ) ;
#92440=VECTOR ( 'NONE', #123330, 1000.000000000000227 ) ;
#92441=DIRECTION ( 'NONE',  ( -0.7071067811865486830, -0.7071067811865464625, 0.000000000000000000 ) ) ;
#92442=AXIS2_PLACEMENT_3D ( 'NONE', #53943, #142363, #200 ) ;
#92443=ORIENTED_EDGE ( 'NONE', *, *, #54043, .T. ) ;
#92444=DIRECTION ( 'NONE',  ( 0.7071067811865487940, 0.7071067811865463515, -0.000000000000000000 ) ) ;
#92445=EDGE_CURVE ( 'NONE', #127400, #133889, #91565, .T. ) ;
#92446=DIRECTION ( 'NONE',  ( 0.7071067811865486830, -0.7071067811865464625, -0.000000000000000000 ) ) ;
#92447=VECTOR ( 'NONE', #98361, 999.9999999999998863 ) ;
#92448=ORIENTED_EDGE ( 'NONE', *, *, #107981, .T. ) ;
#92450=ORIENTED_EDGE ( 'NONE', *, *, #73282, .F. ) ;
#92452=ORIENTED_EDGE ( 'NONE', *, *, #45048, .F. ) ;
#92453=AXIS2_PLACEMENT_3D ( 'NONE', #83279, #82567, #106406 ) ;
#92454=EDGE_CURVE ( 'NONE', #14410, #122126, #16860, .T. ) ;
#92455=VECTOR ( 'NONE', #16922, 1000.000000000000227 ) ;
#92458=VERTEX_POINT ( 'NONE', #105281 ) ;
#92459=ADVANCED_FACE ( 'NONE', ( #93705 ), #103144, .F. ) ;
#92461=EDGE_LOOP ( 'NONE', ( #77788, #83039, #129810, #1574 ) ) ;
#92462=CARTESIAN_POINT ( 'NONE',  ( -60.29974487139158867, -27.71228299555248142, 4.000000000000000000 ) ) ;
#92465=PLANE ( 'NONE',  #15072 ) ;
#92466=LINE ( 'NONE', #133858, #14673 ) ;
#92467=ORIENTED_EDGE ( 'NONE', *, *, #16166, .F. ) ;
#92468=EDGE_LOOP ( 'NONE', ( #3715, #45091, #79296, #119605 ) ) ;
#92469=CARTESIAN_POINT ( 'NONE',  ( -34.75611968250420603, -12.18706574529249842, 4.955485411084898040 ) ) ;
#92470=CARTESIAN_POINT ( 'NONE',  ( -81.29974487139159578, -27.71228299555262709, 4.000000000000000000 ) ) ;
#92471=ORIENTED_EDGE ( 'NONE', *, *, #103869, .T. ) ;
#92473=CARTESIAN_POINT ( 'NONE',  ( -13.82816939922343202, -14.24070752338414003, 4.000000000000000000 ) ) ;
#92475=VERTEX_POINT ( 'NONE', #27721 ) ;
#92477=ORIENTED_EDGE ( 'NONE', *, *, #104390, .F. ) ;
#92478=ORIENTED_EDGE ( 'NONE', *, *, #71175, .T. ) ;
#92480=VECTOR ( 'NONE', #101688, 999.9999999999998863 ) ;
#92481=VECTOR ( 'NONE', #101641, 1000.000000000000000 ) ;
#92482=CARTESIAN_POINT ( 'NONE',  ( 9.792893218813395251, -2.240707523384257716, 5.000000000000000000 ) ) ;
#92483=VECTOR ( 'NONE', #50826, 1000.000000000000000 ) ;
#92485=EDGE_CURVE ( 'NONE', #116152, #46717, #137930, .T. ) ;
#92487=EDGE_CURVE ( 'NONE', #83102, #104888, #127771, .T. ) ;
#92488=VECTOR ( 'NONE', #71356, 1000.000000000000000 ) ;
#92489=FACE_OUTER_BOUND ( 'NONE', #120689, .T. ) ;
#92491=VECTOR ( 'NONE', #61932, 1000.000000000000000 ) ;
#92494=CARTESIAN_POINT ( 'NONE',  ( 29.99999999999979750, -0.2811185226893990752, -5.995736974527582142 ) ) ;
#92496=LINE ( 'NONE', #61370, #139256 ) ;
#92497=VERTEX_POINT ( 'NONE', #108821 ) ;
#92498=ORIENTED_EDGE ( 'NONE', *, *, #65123, .F. ) ;
#92499=VERTEX_POINT ( 'NONE', #107424 ) ;
#92500=PLANE ( 'NONE',  #18586 ) ;
#92502=VECTOR ( 'NONE', #12656, 999.9999999999998863 ) ;
#92504=DIRECTION ( 'NONE',  ( -0.000000000000000000, 0.000000000000000000, 1.000000000000000000 ) ) ;
#92505=CARTESIAN_POINT ( 'NONE',  ( 34.49999999999975842, -4.912538124160710673, 4.000000000000000000 ) ) ;
#92507=EDGE_CURVE ( 'NONE', #110817, #35724, #75524, .T. ) ;
#92510=EDGE_CURVE ( 'NONE', #129125, #96996, #8083, .T. ) ;
#92511=CARTESIAN_POINT ( 'NONE',  ( -65.99451991528749772, 28.92564299267984396, 4.000000000000000000 ) ) ;
#92513=LINE ( 'NONE', #117127, #32587 ) ;
#92514=VERTEX_POINT ( 'NONE', #21124 ) ;
#92515=CARTESIAN_POINT ( 'NONE',  ( 4.499999999999967137, 12.43112307739206024, 4.000000000000000000 ) ) ;
#92516=VERTEX_POINT ( 'NONE', #9507 ) ;
#92517=DIRECTION ( 'NONE',  ( 0.000000000000000000, -0.3543493200069153248, -0.9351131265310291818 ) ) ;
#92519=VERTEX_POINT ( 'NONE', #51639 ) ;
#92520=EDGE_CURVE ( 'NONE', #139777, #24725, #106685, .T. ) ;
#92521=CARTESIAN_POINT ( 'NONE',  ( -36.29974487139159578, -27.71228299555231445, 4.000000000000000000 ) ) ;
#92523=ORIENTED_EDGE ( 'NONE', *, *, #90770, .T. ) ;
#92524=CARTESIAN_POINT ( 'NONE',  ( 13.49999999999990408, -5.568876922607754132, 4.000000000000000000 ) ) ;
#92525=EDGE_LOOP ( 'NONE', ( #2702, #65255, #135617, #101090 ) ) ;
#92526=ORIENTED_EDGE ( 'NONE', *, *, #66912, .F. ) ;
#92527=LINE ( 'NONE', #80974, #126017 ) ;
#92529=LINE ( 'NONE', #25868, #39411 ) ;
#92530=CARTESIAN_POINT ( 'NONE',  ( 11.51078643762690490, -27.52281430457047406, 5.000000000000000000 ) ) ;
#92531=ORIENTED_EDGE ( 'NONE', *, *, #142052, .F. ) ;
#92533=CARTESIAN_POINT ( 'NONE',  ( -0.1349957375162171014, 3.759292476615678336, 15.36553568819726223 ) ) ;
#92534=CARTESIAN_POINT ( 'NONE',  ( 3.241694584251855193, 0.7592924766157104211, 14.37146558664982265 ) ) ;
#92536=DIRECTION ( 'NONE',  ( -0.7071067811865486830, -0.7071067811865464625, 0.000000000000000000 ) ) ;
#92537=PLANE ( 'NONE',  #53601 ) ;
#92538=EDGE_LOOP ( 'NONE', ( #44850, #55229, #118576, #60038 ) ) ;
#92539=CARTESIAN_POINT ( 'NONE',  ( 15.32816939922341426, -15.74070752338413470, 4.000000000000000000 ) ) ;
#92540=VERTEX_POINT ( 'NONE', #52326 ) ;
#92542=CARTESIAN_POINT ( 'NONE',  ( 0.000000000000000000, 0.000000000000000000, 5.000000000000000000 ) ) ;
#92543=FACE_OUTER_BOUND ( 'NONE', #82643, .T. ) ;
#92544=PLANE ( 'NONE',  #118730 ) ;
#92545=LINE ( 'NONE', #62107, #24703 ) ;
#92547=CIRCLE ( 'NONE', #11499, 5.968999999999998529 ) ;
#92548=VECTOR ( 'NONE', #53466, 1000.000000000000000 ) ;
#92549=VECTOR ( 'NONE', #122000, 1000.000000000000114 ) ;
#92550=DIRECTION ( 'NONE',  ( -0.000000000000000000, 0.3543493200069153248, 0.9351131265310292928 ) ) ;
#92551=AXIS2_PLACEMENT_3D ( 'NONE', #43103, #22031, #109764 ) ;
#92553=EDGE_LOOP ( 'NONE', ( #49235, #3360, #85364, #137137 ) ) ;
#92554=FACE_OUTER_BOUND ( 'NONE', #38599, .T. ) ;
#92555=CARTESIAN_POINT ( 'NONE',  ( 14.48334561358944406, 22.22500000000000142, 4.500000000000000888 ) ) ;
#92556=DIRECTION ( 'NONE',  ( -0.3543493200069162685, -0.000000000000000000, -0.9351131265310288487 ) ) ;
#92558=CARTESIAN_POINT ( 'NONE',  ( -34.92500000000001137, 21.72500000000000142, 5.000000000000000000 ) ) ;
#92559=CARTESIAN_POINT ( 'NONE',  ( -34.75611968250421313, 2.812934254707341264, 4.955485411084894487 ) ) ;
#92560=CARTESIAN_POINT ( 'NONE',  ( -34.92500000000001137, -20.99387692260785343, 4.000000000000000000 ) ) ;
#92562=DIRECTION ( 'NONE',  ( -0.7071067811865486830, -0.7071067811865464625, 0.000000000000000000 ) ) ;
#92563=ORIENTED_EDGE ( 'NONE', *, *, #64862, .F. ) ;
#92564=ORIENTED_EDGE ( 'NONE', *, *, #49623, .F. ) ;
#92565=ORIENTED_EDGE ( 'NONE', *, *, #49454, .F. ) ;
#92568=ORIENTED_EDGE ( 'NONE', *, *, #72367, .F. ) ;
#92569=ADVANCED_FACE ( 'NONE', ( #97985 ), #96514, .F. ) ;
#92570=CARTESIAN_POINT ( 'NONE',  ( -42.48921356237308800, -27.52281430457085065, 5.000000000000000000 ) ) ;
#92571=FACE_OUTER_BOUND ( 'NONE', #130113, .T. ) ;
#92572=EDGE_CURVE ( 'NONE', #17308, #30830, #18237, .T. ) ;
#92573=VECTOR ( 'NONE', #877, 1000.000000000000000 ) ;
#92574=DIRECTION ( 'NONE',  ( 0.3543493200069162685, -0.000000000000000000, -0.9351131265310288487 ) ) ;
#92575=DIRECTION ( 'NONE',  ( -0.7071067811865487940, 0.7071067811865463515, -0.000000000000000000 ) ) ;
#92576=ORIENTED_EDGE ( 'NONE', *, *, #80238, .F. ) ;
#92577=ADVANCED_FACE ( 'NONE', ( #85658 ), #120401, .F. ) ;
#92578=FACE_OUTER_BOUND ( 'NONE', #63757, .T. ) ;
#92579=CARTESIAN_POINT ( 'NONE',  ( 0.000000000000000000, -21.72500000000000142, 4.500000000000000888 ) ) ;
#92580=VECTOR ( 'NONE', #44491, 1000.000000000000227 ) ;
#92582=ORIENTED_EDGE ( 'NONE', *, *, #15629, .F. ) ;
#92583=EDGE_CURVE ( 'NONE', #112964, #129502, #74834, .T. ) ;
#92584=LINE ( 'NONE', #23791, #28130 ) ;
#92587=VECTOR ( 'NONE', #68194, 1000.000000000000114 ) ;
#92588=ORIENTED_EDGE ( 'NONE', *, *, #9826, .T. ) ;
#92589=ORIENTED_EDGE ( 'NONE', *, *, #38511, .T. ) ;
#92590=EDGE_CURVE ( 'NONE', #99775, #33858, #140081, .T. ) ;
#92591=DIRECTION ( 'NONE',  ( -0.000000000000000000, 0.000000000000000000, 1.000000000000000000 ) ) ;
#92592=ADVANCED_FACE ( 'NONE', ( #84962 ), #50920, .F. ) ;
#92593=AXIS2_PLACEMENT_3D ( 'NONE', #123100, #110740, #3418 ) ;
#92594=PLANE ( 'NONE',  #54712 ) ;
#92595=DIRECTION ( 'NONE',  ( 0.7071067811865486830, -0.7071067811865464625, -0.000000000000000000 ) ) ;
#92596=AXIS2_PLACEMENT_3D ( 'NONE', #9459, #73350, #65341 ) ;
#92597=DIRECTION ( 'NONE',  ( 0.7071067811865486830, -0.7071067811865464625, -0.000000000000000000 ) ) ;
#92598=ADVANCED_FACE ( 'NONE', ( #142225 ), #30606, .F. ) ;
#92600=CARTESIAN_POINT ( 'NONE',  ( -15.48921356237309510, -27.52281430457066236, 5.000000000000000000 ) ) ;
#92602=AXIS2_PLACEMENT_3D ( 'NONE', #127034, #116173, #37183 ) ;
#92603=ORIENTED_EDGE ( 'NONE', *, *, #33135, .T. ) ;
#92604=ORIENTED_EDGE ( 'NONE', *, *, #55165, .F. ) ;
#92607=ORIENTED_EDGE ( 'NONE', *, *, #93396, .F. ) ;
#92608=AXIS2_PLACEMENT_3D ( 'NONE', #8182, #95934, #61232 ) ;
#92609=PLANE ( 'NONE',  #133106 ) ;
#92610=ORIENTED_EDGE ( 'NONE', *, *, #72877, .T. ) ;
#92612=LINE ( 'NONE', #68770, #140557 ) ;
#92614=CARTESIAN_POINT ( 'NONE',  ( -34.75611968250421313, 17.81293425470718716, 4.955485411084894487 ) ) ;
#92615=AXIS2_PLACEMENT_3D ( 'NONE', #121187, #100867, #134230 ) ;
#92616=CARTESIAN_POINT ( 'NONE',  ( -20.51078643762690490, -27.52281430457041012, 5.000000000000000000 ) ) ;
#92617=EDGE_LOOP ( 'NONE', ( #122425, #64461, #122427, #93404 ) ) ;
#92618=DIRECTION ( 'NONE',  ( -0.6830127018922181881, 0.6830127018922202975, -0.2588190451025214056 ) ) ;
#92619=CARTESIAN_POINT ( 'NONE',  ( 19.05000000000000071, 3.174999999999997158, 4.000000000000000000 ) ) ;
#92620=ORIENTED_EDGE ( 'NONE', *, *, #8372, .F. ) ;
#92621=FACE_OUTER_BOUND ( 'NONE', #45135, .T. ) ;
#92622=ORIENTED_EDGE ( 'NONE', *, *, #92159, .F. ) ;
#92624=CARTESIAN_POINT ( 'NONE',  ( -54.18398860626899705, 28.73617430169825226, 5.000000000000000000 ) ) ;
#92625=ORIENTED_EDGE ( 'NONE', *, *, #59710, .T. ) ;
#92626=EDGE_CURVE ( 'NONE', #15103, #131987, #35618, .T. ) ;
#92627=EDGE_LOOP ( 'NONE', ( #1935, #40501, #103232, #82536 ) ) ;
#92632=PLANE ( 'NONE',  #17175 ) ;
#92634=PLANE ( 'NONE',  #49532 ) ;
#92635=ADVANCED_FACE ( 'NONE', ( #55200 ), #2188, .F. ) ;
#92637=CARTESIAN_POINT ( 'NONE',  ( 13.49999999999990408, -19.53360074219754594, 5.000000000000000000 ) ) ;
#92638=FACE_OUTER_BOUND ( 'NONE', #110913, .T. ) ;
#92640=PLANE ( 'NONE',  #9647 ) ;
#92641=CARTESIAN_POINT ( 'NONE',  ( -31.49999999999977973, -10.53360074219763121, 5.000000000000000000 ) ) ;
#92642=VECTOR ( 'NONE', #17931, 1000.000000000000000 ) ;
#92644=DIRECTION ( 'NONE',  ( 0.7071067811865486830, -0.7071067811865464625, -0.000000000000000000 ) ) ;
#92645=DIRECTION ( 'NONE',  ( -0.6830127018922180770, -0.6830127018922204085, -0.2588190451025213501 ) ) ;
#92647=ORIENTED_EDGE ( 'NONE', *, *, #34700, .F. ) ;
#92648=ORIENTED_EDGE ( 'NONE', *, *, #252, .T. ) ;
#92649=VECTOR ( 'NONE', #103805, 1000.000000000000000 ) ;
#92650=CARTESIAN_POINT ( 'NONE',  ( 23.99999999999983302, -13.97847968911258221, -0.1324546996126253762 ) ) ;
#92651=VECTOR ( 'NONE', #131914, 1000.000000000000227 ) ;
#92652=VECTOR ( 'NONE', #100738, 1000.000000000000000 ) ;
#92653=VERTEX_POINT ( 'NONE', #10240 ) ;
#92654=AXIS2_PLACEMENT_3D ( 'NONE', #7247, #73975, #18859 ) ;
#92655=AXIS2_PLACEMENT_3D ( 'NONE', #86074, #17238, #105647 ) ;
#92656=LINE ( 'NONE', #58684, #23674 ) ;
#92658=EDGE_CURVE ( 'NONE', #16399, #75683, #121843, .T. ) ;
#92659=DIRECTION ( 'NONE',  ( 0.7071067811865487940, 0.7071067811865463515, 0.000000000000000000 ) ) ;
#92660=CARTESIAN_POINT ( 'NONE',  ( 12.72281430457050710, -21.72500000000000142, 5.000000000000000000 ) ) ;
#92661=VERTEX_POINT ( 'NONE', #12384 ) ;
#92662=VECTOR ( 'NONE', #8708, 1000.000000000000000 ) ;
#92663=ORIENTED_EDGE ( 'NONE', *, *, #141272, .F. ) ;
#92664=FACE_OUTER_BOUND ( 'NONE', #59536, .T. ) ;
#92668=EDGE_LOOP ( 'NONE', ( #79178, #119860, #75133, #21686 ) ) ;
#92669=ORIENTED_EDGE ( 'NONE', *, *, #45609, .T. ) ;
#92671=PLANE ( 'NONE',  #116732 ) ;
#92672=VECTOR ( 'NONE', #136963, 1000.000000000000000 ) ;
#92673=CARTESIAN_POINT ( 'NONE',  ( -20.29289321881331176, -3.740707523384246613, 5.000000000000000000 ) ) ;
#92674=CARTESIAN_POINT ( 'NONE',  ( -2.999999999999981792, -8.151047557385073361, -8.977947279169791628 ) ) ;
#92675=CARTESIAN_POINT ( 'NONE',  ( 3.328169399223507519, -3.740707523384244837, 4.000000000000000000 ) ) ;
#92676=ORIENTED_EDGE ( 'NONE', *, *, #41601, .F. ) ;
#92677=LINE ( 'NONE', #49222, #136552 ) ;
#92678=PLANE ( 'NONE',  #38823 ) ;
#92680=VECTOR ( 'NONE', #46523, 1000.000000000000000 ) ;
#92681=CARTESIAN_POINT ( 'NONE',  ( -33.18398860626899705, 28.73617430169810305, 5.000000000000000000 ) ) ;
#92683=LINE ( 'NONE', #57974, #44269 ) ;
#92684=DIRECTION ( 'NONE',  ( 0.7071067811865486830, -0.7071067811865464625, -0.000000000000000000 ) ) ;
#92686=EDGE_LOOP ( 'NONE', ( #114901, #60357, #68877, #45531 ) ) ;
#92687=CARTESIAN_POINT ( 'NONE',  ( 1.499999999999991784, 15.43112307739202471, 4.000000000000000000 ) ) ;
#92688=DIRECTION ( 'NONE',  ( -0.6830127018922181881, 0.6830127018922202975, -0.2588190451025214056 ) ) ;
#92691=CARTESIAN_POINT ( 'NONE',  ( -24.79289321881327979, -20.24070752338407431, 5.000000000000000000 ) ) ;
#92692=EDGE_CURVE ( 'NONE', #36317, #125403, #132054, .T. ) ;
#92693=PLANE ( 'NONE',  #20839 ) ;
#92694=ORIENTED_EDGE ( 'NONE', *, *, #63536, .T. ) ;
#92695=EDGE_LOOP ( 'NONE', ( #89159, #84456, #21590, #13310, #74282 ) ) ;
#92697=EDGE_CURVE ( 'NONE', #72213, #134483, #132786, .T. ) ;
#92698=DIRECTION ( 'NONE',  ( -0.7071067811865486830, -0.7071067811865464625, -0.000000000000000000 ) ) ;
#92699=DIRECTION ( 'NONE',  ( -0.000000000000000000, -0.3543493200069152693, 0.9351131265310292928 ) ) ;
#92701=VERTEX_POINT ( 'NONE', #34886 ) ;
#92702=LINE ( 'NONE', #105008, #72124 ) ;
#92703=ORIENTED_EDGE ( 'NONE', *, *, #28888, .T. ) ;
#92704=CARTESIAN_POINT ( 'NONE',  ( 47.99451991528749062, 28.92564299267971251, 4.000000000000000000 ) ) ;
#92705=LINE ( 'NONE', #112342, #60161 ) ;
#92707=DIRECTION ( 'NONE',  ( -0.000000000000000000, 0.000000000000000000, 1.000000000000000000 ) ) ;
#92708=VECTOR ( 'NONE', #91806, 1000.000000000000000 ) ;
#92709=FACE_OUTER_BOUND ( 'NONE', #113096, .T. ) ;
#92710=PLANE ( 'NONE',  #21328 ) ;
#92712=CARTESIAN_POINT ( 'NONE',  ( 27.32816939922333432, -15.74070752338412760, 4.000000000000000000 ) ) ;
#92714=VECTOR ( 'NONE', #30342, 1000.000000000000000 ) ;
#92716=LINE ( 'NONE', #60866, #8830 ) ;
#92717=CARTESIAN_POINT ( 'NONE',  ( -24.79289321881328334, -14.24070752338413648, 5.000000000000000000 ) ) ;
#92718=CARTESIAN_POINT ( 'NONE',  ( -27.18398860626900060, 28.73617430169806042, 5.000000000000000000 ) ) ;
#92719=ORIENTED_EDGE ( 'NONE', *, *, #59603, .F. ) ;
#92720=EDGE_CURVE ( 'NONE', #80031, #38512, #77673, .T. ) ;
#92724=VERTEX_POINT ( 'NONE', #66086 ) ;
#92725=LINE ( 'NONE', #84044, #66587 ) ;
#92726=LINE ( 'NONE', #102918, #115832 ) ;
#92731=DIRECTION ( 'NONE',  ( 0.7071067811865487940, 0.7071067811865463515, 0.000000000000000000 ) ) ;
#92732=FACE_OUTER_BOUND ( 'NONE', #12962, .T. ) ;
#92734=DIRECTION ( 'NONE',  ( -0.6830127018922181881, 0.6830127018922202975, -0.2588190451025214056 ) ) ;
#92737=DIRECTION ( 'NONE',  ( -0.7071067811865486830, -0.7071067811865464625, 0.000000000000000000 ) ) ;
#92738=VECTOR ( 'NONE', #103932, 1000.000000000000000 ) ;
#92739=CARTESIAN_POINT ( 'NONE',  ( 14.20710678118644665, -17.24070752338410628, 5.000000000000000000 ) ) ;
#92740=DIRECTION ( 'NONE',  ( -0.7071067811865486830, -0.7071067811865464625, 0.000000000000000000 ) ) ;
#92742=DIRECTION ( 'NONE',  ( -0.000000000000000000, 0.000000000000000000, 1.000000000000000000 ) ) ;
#92743=EDGE_LOOP ( 'NONE', ( #44814, #134756, #492, #133386 ) ) ;
#92744=ORIENTED_EDGE ( 'NONE', *, *, #103378, .F. ) ;
#92745=ADVANCED_FACE ( 'NONE', ( #121145 ), #133474, .T. ) ;
#92747=VERTEX_POINT ( 'NONE', #90694 ) ;
#92749=LINE ( 'NONE', #84068, #61726 ) ;
#92750=LINE ( 'NONE', #2895, #64253 ) ;
#92751=ORIENTED_EDGE ( 'NONE', *, *, #67634, .F. ) ;
#92752=EDGE_CURVE ( 'NONE', #83776, #63645, #78379, .T. ) ;
#92753=EDGE_CURVE ( 'NONE', #82669, #127957, #68253, .T. ) ;
#92755=FACE_OUTER_BOUND ( 'NONE', #132858, .T. ) ;
#92756=( BOUNDED_CURVE ( )  B_SPLINE_CURVE ( 3, ( #17759, #16326, #92469, #27221 ),
 .UNSPECIFIED., .F., .F. ) 
 B_SPLINE_CURVE_WITH_KNOTS ( ( 4, 4 ),
 ( 2.779374508378135378, 4.199602562396853145 ),
 .UNSPECIFIED. ) 
 CURVE ( )  GEOMETRIC_REPRESENTATION_ITEM ( )  RATIONAL_B_SPLINE_CURVE ( ( 1.000000000000000000, 0.8388583629366597183, 0.8388583629366597183, 1.000000000000000000 ) ) 
 REPRESENTATION_ITEM ( '' )  );
#92757=VECTOR ( 'NONE', #105108, 1000.000000000000000 ) ;
#92760=ORIENTED_EDGE ( 'NONE', *, *, #57594, .T. ) ;
#92761=ORIENTED_EDGE ( 'NONE', *, *, #52644, .T. ) ;
#92762=DIRECTION ( 'NONE',  ( 0.7071067811865486830, -0.7071067811865464625, -0.000000000000000000 ) ) ;
#92764=VECTOR ( 'NONE', #124453, 1000.000000000000000 ) ;
#92766=CARTESIAN_POINT ( 'NONE',  ( -30.79289321881323360, 12.75929247661558463, 5.000000000000000000 ) ) ;
#92769=ORIENTED_EDGE ( 'NONE', *, *, #42727, .T. ) ;
#92770=EDGE_LOOP ( 'NONE', ( #88023, #29229, #94540, #93857 ) ) ;
#92771=EDGE_CURVE ( 'NONE', #7159, #78369, #33472, .T. ) ;
#92772=ORIENTED_EDGE ( 'NONE', *, *, #45649, .T. ) ;
#92773=FACE_OUTER_BOUND ( 'NONE', #12940, .T. ) ;
#92774=ADVANCED_FACE ( 'NONE', ( #109565 ), #54501, .F. ) ;
#92779=VERTEX_POINT ( 'NONE', #81976 ) ;
#92780=VECTOR ( 'NONE', #2926, 999.9999999999998863 ) ;
#92781=DIRECTION ( 'NONE',  ( -0.000000000000000000, 0.3543493200069153248, 0.9351131265310292928 ) ) ;
#92782=ORIENTED_EDGE ( 'NONE', *, *, #43142, .F. ) ;
#92784=AXIS2_PLACEMENT_3D ( 'NONE', #108533, #18686, #74544 ) ;
#92785=EDGE_CURVE ( 'NONE', #134614, #66046, #36300, .T. ) ;
#92786=DIRECTION ( 'NONE',  ( 0.6830127018922181881, 0.6830127018922202975, -0.2588190451025214056 ) ) ;
#92787=AXIS2_PLACEMENT_3D ( 'NONE', #118251, #29822, #97957 ) ;
#92788=VECTOR ( 'NONE', #115545, 1000.000000000000227 ) ;
#92789=DIRECTION ( 'NONE',  ( 0.3543493200069162685, -0.000000000000000000, -0.9351131265310288487 ) ) ;
#92790=EDGE_LOOP ( 'NONE', ( #26866, #137714, #82627, #101381 ) ) ;
#92791=DIRECTION ( 'NONE',  ( 0.3543493200069162685, -0.000000000000000000, -0.9351131265310288487 ) ) ;
#92792=VECTOR ( 'NONE', #76916, 1000.000000000000000 ) ;
#92793=CARTESIAN_POINT ( 'NONE',  ( -23.21837311707488993, 21.74787736706806029, 4.999607392498049308 ) ) ;
#92794=EDGE_CURVE ( 'NONE', #130142, #110486, #105112, .T. ) ;
#92795=PLANE ( 'NONE',  #46043 ) ;
#92796=VECTOR ( 'NONE', #90785, 1000.000000000000000 ) ;
#92797=DIRECTION ( 'NONE',  ( -0.7071067811865487940, 0.7071067811865463515, -0.000000000000000000 ) ) ;
#92799=FACE_BOUND ( 'NONE', #48866, .T. ) ;
#92800=ORIENTED_EDGE ( 'NONE', *, *, #25058, .F. ) ;
#92801=CARTESIAN_POINT ( 'NONE',  ( -3.005480084712505828, 28.92564299267936079, 4.000000000000000000 ) ) ;
#92802=CARTESIAN_POINT ( 'NONE',  ( 47.99451991528749062, 28.92564299267971251, 4.000000000000000000 ) ) ;
#92805=ORIENTED_EDGE ( 'NONE', *, *, #52842, .F. ) ;
#92806=EDGE_CURVE ( 'NONE', #24327, #49400, #2937, .T. ) ;
#92807=LINE ( 'NONE', #68953, #131618 ) ;
#92808=ORIENTED_EDGE ( 'NONE', *, *, #138854, .F. ) ;
#92809=ORIENTED_EDGE ( 'NONE', *, *, #132739, .T. ) ;
#92810=ORIENTED_EDGE ( 'NONE', *, *, #133117, .T. ) ;
#92811=EDGE_CURVE ( 'NONE', #104032, #106976, #115966, .T. ) ;
#92813=ORIENTED_EDGE ( 'NONE', *, *, #100813, .T. ) ;
#92814=AXIS2_PLACEMENT_3D ( 'NONE', #60757, #38251, #115756 ) ;
#92815=DIRECTION ( 'NONE',  ( -0.7071067811865486830, -0.7071067811865464625, 0.000000000000000000 ) ) ;
#92816=DIRECTION ( 'NONE',  ( -0.7071067811865486830, 0.7071067811865464625, 0.000000000000000000 ) ) ;
#92817=DIRECTION ( 'NONE',  ( -0.6830127018922180770, -0.6830127018922204085, -0.2588190451025213501 ) ) ;
#92818=ORIENTED_EDGE ( 'NONE', *, *, #42046, .T. ) ;
#92821=DIRECTION ( 'NONE',  ( 0.6830127018922180770, -0.6830127018922204085, -0.2588190451025213501 ) ) ;
#92823=DIRECTION ( 'NONE',  ( 0.7071067811865487940, 0.7071067811865463515, -0.000000000000000000 ) ) ;
#92824=CARTESIAN_POINT ( 'NONE',  ( 2.999999999999983569, 19.93112307739198030, 4.000000000000000000 ) ) ;
#92825=DIRECTION ( 'NONE',  ( 0.7071067811865487940, 0.7071067811865463515, 0.000000000000000000 ) ) ;
#92826=DIRECTION ( 'NONE',  ( 0.6830127018922181881, 0.6830127018922202975, -0.2588190451025214056 ) ) ;
#92827=LINE ( 'NONE', #50762, #61048 ) ;
#92829=VERTEX_POINT ( 'NONE', #59498 ) ;
#92830=ORIENTED_EDGE ( 'NONE', *, *, #53984, .T. ) ;
#92831=VECTOR ( 'NONE', #26541, 1000.000000000000000 ) ;
#92832=VERTEX_POINT ( 'NONE', #36994 ) ;
#92834=EDGE_LOOP ( 'NONE', ( #44975, #26938, #74656, #112324 ) ) ;
#92835=ORIENTED_EDGE ( 'NONE', *, *, #70653, .T. ) ;
#92836=DIRECTION ( 'NONE',  ( 0.7071067811865487940, 0.7071067811865463515, 0.000000000000000000 ) ) ;
#92837=DIRECTION ( 'NONE',  ( 0.6830127018922180770, -0.6830127018922204085, -0.2588190451025213501 ) ) ;
#92838=CARTESIAN_POINT ( 'NONE',  ( 48.18398860626899705, 28.73617430169820608, 5.000000000000000000 ) ) ;
#92842=ORIENTED_EDGE ( 'NONE', *, *, #115303, .F. ) ;
#92843=CARTESIAN_POINT ( 'NONE',  ( -60.48921356237309510, -27.52281430457097500, 5.000000000000000000 ) ) ;
#92846=ORIENTED_EDGE ( 'NONE', *, *, #109766, .F. ) ;
#92848=LINE ( 'NONE', #4349, #18879 ) ;
#92849=FACE_OUTER_BOUND ( 'NONE', #50720, .T. ) ;
#92850=EDGE_CURVE ( 'NONE', #77053, #67112, #70404, .T. ) ;
#92851=ORIENTED_EDGE ( 'NONE', *, *, #102761, .T. ) ;
#92852=ORIENTED_EDGE ( 'NONE', *, *, #18812, .F. ) ;
#92853=SURFACE_SIDE_STYLE ('',( #28337 ) ) ;
#92854=ORIENTED_EDGE ( 'NONE', *, *, #30229, .F. ) ;
#92855=LINE ( 'NONE', #124779, #115784 ) ;
#92857=VECTOR ( 'NONE', #48652, 1000.000000000000227 ) ;
#92858=LINE ( 'NONE', #80589, #60937 ) ;
#92859=ORIENTED_EDGE ( 'NONE', *, *, #17173, .F. ) ;
#92860=VECTOR ( 'NONE', #69311, 999.9999999999998863 ) ;
#92862=VECTOR ( 'NONE', #48764, 1000.000000000000000 ) ;
#92863=CARTESIAN_POINT ( 'NONE',  ( -20.99999999999984723, -8.731860332648860634, -2.120594902707586549 ) ) ;
#92864=LINE ( 'NONE', #137102, #81592 ) ;
#92865=ORIENTED_EDGE ( 'NONE', *, *, #134840, .F. ) ;
#92866=DIRECTION ( 'NONE',  ( -0.7071067811865486830, -0.7071067811865464625, 0.000000000000000000 ) ) ;
#92868=VECTOR ( 'NONE', #69210, 1000.000000000000227 ) ;
#92869=AXIS2_PLACEMENT_3D ( 'NONE', #71160, #27620, #72618 ) ;
#92870=AXIS2_PLACEMENT_3D ( 'NONE', #94886, #84073, #73186 ) ;
#92871=CARTESIAN_POINT ( 'NONE',  ( 8.671830600776420539, 17.25929247661555266, 4.000000000000000000 ) ) ;
#92872=VECTOR ( 'NONE', #32059, 1000.000000000000000 ) ;
#92873=ORIENTED_EDGE ( 'NONE', *, *, #84605, .T. ) ;
#92874=ADVANCED_FACE ( 'NONE', ( #125452 ), #82663, .F. ) ;
#92875=DIRECTION ( 'NONE',  ( 0.6830127018922181881, 0.6830127018922202975, -0.2588190451025214056 ) ) ;
#92876=ORIENTED_EDGE ( 'NONE', *, *, #108484, .F. ) ;
#92877=ADVANCED_FACE ( 'NONE', ( #138469 ), #71085, .F. ) ;
#92878=ORIENTED_EDGE ( 'NONE', *, *, #82850, .F. ) ;
#92880=AXIS2_PLACEMENT_3D ( 'NONE', #82967, #4609, #125031 ) ;
#92881=LINE ( 'NONE', #71879, #106224 ) ;
#92882=EDGE_LOOP ( 'NONE', ( #38184, #63918, #114909, #3929 ) ) ;
#92883=LINE ( 'NONE', #18889, #69736 ) ;
#92884=FACE_OUTER_BOUND ( 'NONE', #25237, .T. ) ;
#92886=EDGE_LOOP ( 'NONE', ( #134335, #125232, #114586, #25935, #58456, #136278 ) ) ;
#92887=EDGE_CURVE ( 'NONE', #28959, #141805, #39154, .T. ) ;
#92888=VECTOR ( 'NONE', #89593, 1000.000000000000000 ) ;
#92889=LINE ( 'NONE', #82060, #43886 ) ;
#92890=DIRECTION ( 'NONE',  ( -0.6830127018922180770, -0.6830127018922204085, -0.2588190451025213501 ) ) ;
#92891=PLANE ( 'NONE',  #37489 ) ;
#92892=PLANE ( 'NONE',  #79491 ) ;
#92893=DIRECTION ( 'NONE',  ( -0.7071067811865486830, -0.7071067811865464625, 0.000000000000000000 ) ) ;
#92894=CARTESIAN_POINT ( 'NONE',  ( 7.499999999999951150, 16.18958161055403622, -11.56426086740809644 ) ) ;
#92896=LINE ( 'NONE', #92169, #66243 ) ;
#92897=ORIENTED_EDGE ( 'NONE', *, *, #45482, .T. ) ;
#92898=ADVANCED_FACE ( 'NONE', ( #26136 ), #69666, .F. ) ;
#92900=ORIENTED_EDGE ( 'NONE', *, *, #139148, .F. ) ;
#92901=ORIENTED_EDGE ( 'NONE', *, *, #19200, .F. ) ;
#92903=VECTOR ( 'NONE', #40553, 1000.000000000000000 ) ;
#92904=ORIENTED_EDGE ( 'NONE', *, *, #69261, .F. ) ;
#92906=AXIS2_PLACEMENT_3D ( 'NONE', #88215, #33841, #20064 ) ;
#92908=DIRECTION ( 'NONE',  ( 0.7071067811865487940, -0.7071067811865463515, 0.000000000000000000 ) ) ;
#92909=DIRECTION ( 'NONE',  ( 0.3543493200069162685, -0.000000000000000000, -0.9351131265310288487 ) ) ;
#92910=EDGE_CURVE ( 'NONE', #134985, #49111, #4297, .T. ) ;
#92911=EDGE_CURVE ( 'NONE', #31004, #42434, #5046, .T. ) ;
#92913=EDGE_LOOP ( 'NONE', ( #86619, #30404, #42544, #68432 ) ) ;
#92914=CARTESIAN_POINT ( 'NONE',  ( 45.48921356237309510, -27.52281430457087197, 5.000000000000000000 ) ) ;
#92915=FACE_OUTER_BOUND ( 'NONE', #90902, .T. ) ;
#92916=DIRECTION ( 'NONE',  ( 0.7071067811865487940, 0.7071067811865463515, 0.000000000000000000 ) ) ;
#92918=AXIS2_PLACEMENT_3D ( 'NONE', #40342, #18523, #130194 ) ;
#92919=ORIENTED_EDGE ( 'NONE', *, *, #103131, .F. ) ;
#92920=LINE ( 'NONE', #50147, #83523 ) ;
#92921=CARTESIAN_POINT ( 'NONE',  ( 27.18398860626900060, 28.73617430169806042, 5.000000000000000000 ) ) ;
#92923=DIRECTION ( 'NONE',  ( -0.6830127018922181881, 0.6830127018922202975, -0.2588190451025214056 ) ) ;
#92924=CARTESIAN_POINT ( 'NONE',  ( 8.999999999999937828, 1.761378380278691314, -6.096875308897234724 ) ) ;
#92926=LINE ( 'NONE', #116097, #39860 ) ;
#92927=PLANE ( 'NONE',  #18364 ) ;
#92928=AXIS2_PLACEMENT_3D ( 'NONE', #78726, #46117, #112768 ) ;
#92929=ORIENTED_EDGE ( 'NONE', *, *, #85407, .T. ) ;
#92930=VERTEX_POINT ( 'NONE', #137033 ) ;
#92932=ORIENTED_EDGE ( 'NONE', *, *, #42522, .F. ) ;
#92933=ORIENTED_EDGE ( 'NONE', *, *, #45139, .T. ) ;
#92934=CARTESIAN_POINT ( 'NONE',  ( -14.99451991528749595, 28.92564299267948513, 4.000000000000000000 ) ) ;
#92936=VECTOR ( 'NONE', #10894, 1000.000000000000227 ) ;
#92937=DIRECTION ( 'NONE',  ( -0.7071067811865486830, -0.7071067811865464625, 0.000000000000000000 ) ) ;
#92938=VERTEX_POINT ( 'NONE', #14541 ) ;
#92940=LINE ( 'NONE', #13213, #75643 ) ;
#92941=CARTESIAN_POINT ( 'NONE',  ( 33.18398860626899705, 28.73617430169810305, 5.000000000000000000 ) ) ;
#92942=EDGE_CURVE ( 'NONE', #116108, #93902, #97803, .T. ) ;
#92943=EDGE_CURVE ( 'NONE', #21885, #139855, #107246, .T. ) ;
#92946=EDGE_LOOP ( 'NONE', ( #21977, #31944, #15693, #62315 ) ) ;
#92947=DIRECTION ( 'NONE',  ( -0.7071067811865486830, -0.7071067811865464625, 0.000000000000000000 ) ) ;
#92948=ORIENTED_EDGE ( 'NONE', *, *, #108009, .F. ) ;
#92949=AXIS2_PLACEMENT_3D ( 'NONE', #117457, #97880, #21011 ) ;
#92951=EDGE_CURVE ( 'NONE', #143112, #121799, #7190, .T. ) ;
#92952=LINE ( 'NONE', #16824, #105512 ) ;
#92954=DIRECTION ( 'NONE',  ( -0.7071067811865486830, 0.7071067811865464625, 0.000000000000000000 ) ) ;
#92955=EDGE_LOOP ( 'NONE', ( #61541, #128456, #98893, #84764 ) ) ;
#92956=EDGE_CURVE ( 'NONE', #42124, #116559, #129000, .T. ) ;
#92958=CARTESIAN_POINT ( 'NONE',  ( 6.183988606268994381, 28.73617430169791476, 5.000000000000000000 ) ) ;
#92960=CARTESIAN_POINT ( 'NONE',  ( -5.292893218813420120, -9.740707523384182664, 5.000000000000000000 ) ) ;
#92961=CARTESIAN_POINT ( 'NONE',  ( -18.48921356237309510, -27.52281430457068367, 5.000000000000000000 ) ) ;
#92962=AXIS2_PLACEMENT_3D ( 'NONE', #100051, #108735, #121770 ) ;
#92963=( BOUNDED_CURVE ( )  B_SPLINE_CURVE ( 3, ( #7675, #9828, #119985, #119296 ),
 .UNSPECIFIED., .F., .T. ) 
 B_SPLINE_CURVE_WITH_KNOTS ( ( 4, 4 ),
 ( 1.864375635226946049, 1.933014472006540752 ),
 .UNSPECIFIED. ) 
 CURVE ( )  GEOMETRIC_REPRESENTATION_ITEM ( )  RATIONAL_B_SPLINE_CURVE ( ( 1.000000000000000000, 0.9996074310407766506, 0.9996074310407766506, 1.000000000000000000 ) ) 
 REPRESENTATION_ITEM ( '' )  );
#92964=EDGE_CURVE ( 'NONE', #103024, #69036, #95655, .T. ) ;
#92967=EDGE_LOOP ( 'NONE', ( #6340, #58870, #69129, #112743 ) ) ;
#92969=CARTESIAN_POINT ( 'NONE',  ( 35.99451991528749772, 28.92564299267963079, 4.000000000000000000 ) ) ;
#92970=ORIENTED_EDGE ( 'NONE', *, *, #65362, .F. ) ;
#92971=ORIENTED_EDGE ( 'NONE', *, *, #76454, .T. ) ;
#92972=CARTESIAN_POINT ( 'NONE',  ( 39.18398860626899705, 28.73617430169814568, 5.000000000000000000 ) ) ;
#92974=ADVANCED_FACE ( 'NONE', ( #50742 ), #20220, .F. ) ;
#92976=VECTOR ( 'NONE', #74306, 1000.000000000000000 ) ;
#92978=DIRECTION ( 'NONE',  ( 0.7071067811865487940, 0.7071067811865463515, 0.000000000000000000 ) ) ;
#92979=ORIENTED_EDGE ( 'NONE', *, *, #56613, .F. ) ;
#92980=CARTESIAN_POINT ( 'NONE',  ( -39.18398860626899705, 28.73617430169814568, 5.000000000000000000 ) ) ;
#92981=VECTOR ( 'NONE', #42636, 1000.000000000000000 ) ;
#92982=VECTOR ( 'NONE', #2298, 999.9999999999998863 ) ;
#92983=CARTESIAN_POINT ( 'NONE',  ( 63.48921356237309510, -27.52281430457099631, 5.000000000000000000 ) ) ;
#92985=VECTOR ( 'NONE', #123828, 1000.000000000000000 ) ;
#92987=DIRECTION ( 'NONE',  ( -0.3543493200069162685, -0.000000000000000000, -0.9351131265310288487 ) ) ;
#92988=FACE_BOUND ( 'NONE', #84976, .T. ) ;
#92990=CARTESIAN_POINT ( 'NONE',  ( 34.47516574401890921, 10.49051761211551437, 4.998110765256833510 ) ) ;
#92991=VECTOR ( 'NONE', #136103, 1000.000000000000000 ) ;
#92992=LINE ( 'NONE', #13973, #94439 ) ;
#92993=CARTESIAN_POINT ( 'NONE',  ( -14.20003122016828101, 8.259292476615634371, 16.85664084051844469 ) ) ;
#92994=ORIENTED_EDGE ( 'NONE', *, *, #139883, .T. ) ;
#92995=CARTESIAN_POINT ( 'NONE',  ( -4.171830600776443632, 15.75929247661556332, 4.000000000000000000 ) ) ;
#92996=EDGE_LOOP ( 'NONE', ( #103392, #26209, #140687, #76831 ) ) ;
#92997=EDGE_CURVE ( 'NONE', #106040, #102218, #29677, .T. ) ;
#92998=ADVANCED_FACE ( 'NONE', ( #73917 ), #116705, .F. ) ;
#92999=ORIENTED_EDGE ( 'NONE', *, *, #67581, .F. ) ;
#93001=ORIENTED_EDGE ( 'NONE', *, *, #132742, .T. ) ;
#93002=CARTESIAN_POINT ( 'NONE',  ( 57.48921356237308800, -27.52281430457095368, 5.000000000000000000 ) ) ;
#93003=DIRECTION ( 'NONE',  ( 0.7071067811865487940, 0.7071067811865463515, 0.000000000000000000 ) ) ;
#93004=ORIENTED_EDGE ( 'NONE', *, *, #72299, .F. ) ;
#93005=CARTESIAN_POINT ( 'NONE',  ( -34.92500000000001137, -22.22500000000000142, 4.500000000000000888 ) ) ;
#93006=EDGE_CURVE ( 'NONE', #109576, #78218, #73222, .T. ) ;
#93009=LINE ( 'NONE', #137236, #94201 ) ;
#93010=FACE_OUTER_BOUND ( 'NONE', #96929, .T. ) ;
#93011=FACE_OUTER_BOUND ( 'NONE', #108116, .T. ) ;
#93012=VECTOR ( 'NONE', #82695, 1000.000000000000000 ) ;
#93013=CARTESIAN_POINT ( 'NONE',  ( -11.29289321881337571, -18.74070752338409562, 5.000000000000000000 ) ) ;
#93014=ORIENTED_EDGE ( 'NONE', *, *, #35845, .T. ) ;
#93016=AXIS2_PLACEMENT_3D ( 'NONE', #68367, #88669, #43715 ) ;
#93017=PLANE ( 'NONE',  #33510 ) ;
#93018=CARTESIAN_POINT ( 'NONE',  ( 0.000000000000000000, 0.000000000000000000, 5.000000000000000000 ) ) ;
#93020=ORIENTED_EDGE ( 'NONE', *, *, #76032, .F. ) ;
#93021=ORIENTED_EDGE ( 'NONE', *, *, #41090, .F. ) ;
#93022=DIRECTION ( 'NONE',  ( 0.6830127018922181881, 0.6830127018922202975, -0.2588190451025214056 ) ) ;
#93023=CARTESIAN_POINT ( 'NONE',  ( -3.489213562373097322, -27.52281430457057709, 5.000000000000000000 ) ) ;
#93026=AXIS2_PLACEMENT_3D ( 'NONE', #126341, #70585, #35807 ) ;
#93028=DIRECTION ( 'NONE',  ( -0.000000000000000000, -0.3543493200069152693, 0.9351131265310292928 ) ) ;
#93029=VERTEX_POINT ( 'NONE', #52160 ) ;
#93030=FACE_OUTER_BOUND ( 'NONE', #119682, .T. ) ;
#93033=VECTOR ( 'NONE', #100637, 1000.000000000000227 ) ;
#93034=CARTESIAN_POINT ( 'NONE',  ( -31.49999999999977973, -2.568876922607794988, 4.000000000000000000 ) ) ;
#93035=CARTESIAN_POINT ( 'NONE',  ( -30.18398860626900060, 28.73617430169808173, 5.000000000000000000 ) ) ;
#93036=ORIENTED_EDGE ( 'NONE', *, *, #112617, .F. ) ;
#93037=CARTESIAN_POINT ( 'NONE',  ( -7.499999999999951150, 14.14708470758590408, -0.5283514160166384865 ) ) ;
#93038=VECTOR ( 'NONE', #46595, 1000.000000000000000 ) ;
#93040=DIRECTION ( 'NONE',  ( -0.000000000000000000, -0.3543493200069152693, 0.9351131265310292928 ) ) ;
#93041=CARTESIAN_POINT ( 'NONE',  ( -34.92500000000001137, -22.22500000000000142, 4.000000000000000000 ) ) ;
#93043=ORIENTED_EDGE ( 'NONE', *, *, #3919, .F. ) ;
#93044=DIRECTION ( 'NONE',  ( 0.3543493200069162685, -0.000000000000000000, -0.9351131265310288487 ) ) ;
#93045=EDGE_CURVE ( 'NONE', #77094, #86149, #100501, .T. ) ;
#93046=CARTESIAN_POINT ( 'NONE',  ( -51.29974487139158867, -27.71228299555242103, 4.000000000000000000 ) ) ;
#93047=CARTESIAN_POINT ( 'NONE',  ( 34.92499999999998295, 2.718490437204236443, 4.759050581649325373 ) ) ;
#93048=LINE ( 'NONE', #39397, #81492 ) ;
#93049=VECTOR ( 'NONE', #97286, 1000.000000000000000 ) ;
#93050=EDGE_LOOP ( 'NONE', ( #59192, #123067, #83125, #71901 ) ) ;
#93051=DIRECTION ( 'NONE',  ( 0.3543493200069162685, -0.000000000000000000, -0.9351131265310288487 ) ) ;
#93052=CARTESIAN_POINT ( 'NONE',  ( -32.99999999999977263, -8.151047557385101783, -8.977947279169725903 ) ) ;
#93056=DIRECTION ( 'NONE',  ( 0.3543493200069162685, -0.000000000000000000, -0.9351131265310288487 ) ) ;
#93058=VERTEX_POINT ( 'NONE', #33823 ) ;
#93059=ORIENTED_EDGE ( 'NONE', *, *, #60897, .F. ) ;
#93061=FACE_OUTER_BOUND ( 'NONE', #140961, .T. ) ;
#93062=DIRECTION ( 'NONE',  ( -0.7071067811865486830, -0.7071067811865464625, 0.000000000000000000 ) ) ;
#93063=EDGE_CURVE ( 'NONE', #107560, #11112, #70050, .T. ) ;
#93064=ADVANCED_FACE ( 'NONE', ( #122219 ), #46134, .F. ) ;
#93066=DIRECTION ( 'NONE',  ( -0.7071067811865487940, 0.7071067811865463515, 0.000000000000000000 ) ) ;
#93068=CARTESIAN_POINT ( 'NONE',  ( 48.48921356237309510, -27.52281430457089328, 5.000000000000000000 ) ) ;
#93069=DIRECTION ( 'NONE',  ( 0.6830127018922181881, 0.6830127018922202975, -0.2588190451025214056 ) ) ;
#93070=ORIENTED_EDGE ( 'NONE', *, *, #25360, .T. ) ;
#93071=ADVANCED_FACE ( 'NONE', ( #35971 ), #12036, .F. ) ;
#93072=CARTESIAN_POINT ( 'NONE',  ( -14.00492477221185972, -5.240707523384228850, 12.38332538355499146 ) ) ;
#93073=DIRECTION ( 'NONE',  ( -0.6830127018922181881, 0.6830127018922202975, -0.2588190451025214056 ) ) ;
#93074=VECTOR ( 'NONE', #119780, 999.9999999999998863 ) ;
#93075=AXIS2_PLACEMENT_3D ( 'NONE', #92121, #68293, #124767 ) ;
#93076=FACE_OUTER_BOUND ( 'NONE', #105578, .T. ) ;
#93078=PLANE ( 'NONE',  #14042 ) ;
#93079=VECTOR ( 'NONE', #77, 1000.000000000000227 ) ;
#93080=EDGE_CURVE ( 'NONE', #26531, #89946, #113484, .T. ) ;
#93083=CYLINDRICAL_SURFACE ( 'NONE', #32615, 0.5000000000000004441 ) ;
#93084=ORIENTED_EDGE ( 'NONE', *, *, #47054, .T. ) ;
#93086=VECTOR ( 'NONE', #101845, 1000.000000000000000 ) ;
#93089=EDGE_CURVE ( 'NONE', #113425, #129006, #101913, .T. ) ;
#93090=CARTESIAN_POINT ( 'NONE',  ( -0.1839886062690032631, 28.73617430169787568, 5.000000000000000000 ) ) ;
#93091=DIRECTION ( 'NONE',  ( 0.7071067811865487940, -0.7071067811865463515, 0.000000000000000000 ) ) ;
#93092=PLANE ( 'NONE',  #90245 ) ;
#93093=LINE ( 'NONE', #72094, #30241 ) ;
#93094=CARTESIAN_POINT ( 'NONE',  ( 48.18398860626899705, 28.73617430169820608, 5.000000000000000000 ) ) ;
#93095=ORIENTED_EDGE ( 'NONE', *, *, #72351, .F. ) ;
#93096=FACE_OUTER_BOUND ( 'NONE', #65212, .T. ) ;
#93098=EDGE_CURVE ( 'NONE', #118931, #88406, #46884, .T. ) ;
#93100=CARTESIAN_POINT ( 'NONE',  ( 21.48921356237309155, -27.52281430457070499, 5.000000000000000000 ) ) ;
#93101=CARTESIAN_POINT ( 'NONE',  ( -34.49999999999975842, 12.05432934483081553, 4.994342998332167660 ) ) ;
#93103=CARTESIAN_POINT ( 'NONE',  ( -77.99451991528749772, 28.92564299267992567, 4.000000000000000000 ) ) ;
#93104=ORIENTED_EDGE ( 'NONE', *, *, #29054, .F. ) ;
#93105=EDGE_LOOP ( 'NONE', ( #41987, #132037, #717, #131881 ) ) ;
#93107=CARTESIAN_POINT ( 'NONE',  ( -20.95341186370443154, 14.25929247661556332, 18.84478104361332385 ) ) ;
#93108=CARTESIAN_POINT ( 'NONE',  ( 0.000000000000000000, 0.000000000000000000, 5.000000000000000000 ) ) ;
#93110=EDGE_CURVE ( 'NONE', #143315, #39146, #71226, .T. ) ;
#93114=ADVANCED_FACE ( 'NONE', ( #138839 ), #28658, .T. ) ;
#93115=VECTOR ( 'NONE', #77829, 999.9999999999998863 ) ;
#93116=DIRECTION ( 'NONE',  ( -1.000000000000000000, 7.120242111146219159E-15, 0.000000000000000000 ) ) ;
#93118=ADVANCED_FACE ( 'NONE', ( #84471 ), #94587, .F. ) ;
#93119=VECTOR ( 'NONE', #33345, 1000.000000000000000 ) ;
#93120=DIRECTION ( 'NONE',  ( -0.3543493200069162685, -0.000000000000000000, -0.9351131265310288487 ) ) ;
#93121=VERTEX_POINT ( 'NONE', #126502 ) ;
#93122=VERTEX_POINT ( 'NONE', #29334 ) ;
#93123=VECTOR ( 'NONE', #85427, 1000.000000000000000 ) ;
#93124=DIRECTION ( 'NONE',  ( 0.7071067811865487940, -0.7071067811865463515, 0.000000000000000000 ) ) ;
#93125=EDGE_CURVE ( 'NONE', #122891, #6488, #114891, .T. ) ;
#93126=CARTESIAN_POINT ( 'NONE',  ( 23.99999999999983302, -4.068876922607771895, 4.000000000000000000 ) ) ;
#93127=FACE_OUTER_BOUND ( 'NONE', #22410, .T. ) ;
#93128=CARTESIAN_POINT ( 'NONE',  ( -36.18398860626899705, 28.73617430169812437, 5.000000000000000000 ) ) ;
#93129=DIRECTION ( 'NONE',  ( 0.7071067811865487940, 0.7071067811865463515, 0.000000000000000000 ) ) ;
#93130=ORIENTED_EDGE ( 'NONE', *, *, #17529, .T. ) ;
#93132=CARTESIAN_POINT ( 'NONE',  ( 27.48921356237309155, -27.52281430457074762, 5.000000000000000000 ) ) ;
#93133=DIRECTION ( 'NONE',  ( -0.6830127018922181881, 0.6830127018922202975, -0.2588190451025214056 ) ) ;
#93136=ORIENTED_EDGE ( 'NONE', *, *, #27571, .T. ) ;
#93137=ORIENTED_EDGE ( 'NONE', *, *, #86824, .T. ) ;
#93138=EDGE_CURVE ( 'NONE', #116001, #84730, #59850, .T. ) ;
#93139=CARTESIAN_POINT ( 'NONE',  ( 0.000000000000000000, 0.000000000000000000, 5.000000000000000000 ) ) ;
#93140=CARTESIAN_POINT ( 'NONE',  ( -34.49999999999975842, -15.29013452822857388, 0.3645803511609551073 ) ) ;
#93141=AXIS2_PLACEMENT_3D ( 'NONE', #102612, #136634, #37345 ) ;
#93142=DIRECTION ( 'NONE',  ( -0.6830127018922180770, -0.6830127018922204085, -0.2588190451025213501 ) ) ;
#93144=ORIENTED_EDGE ( 'NONE', *, *, #30517, .T. ) ;
#93145=ORIENTED_EDGE ( 'NONE', *, *, #96319, .F. ) ;
#93147=LINE ( 'NONE', #17015, #42191 ) ;
#93148=EDGE_CURVE ( 'NONE', #133007, #109272, #15569, .T. ) ;
#93149=ORIENTED_EDGE ( 'NONE', *, *, #126323, .T. ) ;
#93150=CARTESIAN_POINT ( 'NONE',  ( 3.793339364578457662, 21.75929247661549937, 4.998822639870711626 ) ) ;
#93153=PLANE ( 'NONE',  #67948 ) ;
#93154=AXIS2_PLACEMENT_3D ( 'NONE', #114447, #80427, #113013 ) ;
#93156=FACE_BOUND ( 'NONE', #82913, .T. ) ;
#93157=CARTESIAN_POINT ( 'NONE',  ( 19.49999999999986500, -5.568876922607755908, 4.000000000000000000 ) ) ;
#93158=DIRECTION ( 'NONE',  ( -0.7071067811865487940, 0.7071067811865463515, -0.000000000000000000 ) ) ;
#93159=CARTESIAN_POINT ( 'NONE',  ( -16.17183060077635304, 12.75929247661558286, 4.000000000000000000 ) ) ;
#93161=CARTESIAN_POINT ( 'NONE',  ( 0.000000000000000000, 0.000000000000000000, 5.000000000000000000 ) ) ;
#93162=CARTESIAN_POINT ( 'NONE',  ( 0.000000000000000000, 0.000000000000000000, 5.000000000000000000 ) ) ;
#93165=EDGE_CURVE ( 'NONE', #25917, #68002, #83765, .T. ) ;
#93166=ORIENTED_EDGE ( 'NONE', *, *, #129288, .F. ) ;
#93168=VERTEX_POINT ( 'NONE', #7574 ) ;
#93169=FACE_OUTER_BOUND ( 'NONE', #35525, .T. ) ;
#93170=CARTESIAN_POINT ( 'NONE',  ( 22.88959668761254207, -22.22500000000000142, -16.90811190805141706 ) ) ;
#93171=VECTOR ( 'NONE', #33551, 1000.000000000000000 ) ;
#93172=AXIS2_PLACEMENT_3D ( 'NONE', #37539, #36799, #48391 ) ;
#93173=VECTOR ( 'NONE', #117773, 1000.000000000000000 ) ;
#93174=VECTOR ( 'NONE', #106510, 999.9999999999998863 ) ;
#93175=LINE ( 'NONE', #6117, #14691 ) ;
#93176=EDGE_LOOP ( 'NONE', ( #48373, #30471, #5248, #129811 ) ) ;
#93177=CARTESIAN_POINT ( 'NONE',  ( 1.734723475976807094E-15, -19.22509904557636418, 1.855685503482177978 ) ) ;
#93178=FACE_OUTER_BOUND ( 'NONE', #88736, .T. ) ;
#93179=DIRECTION ( 'NONE',  ( -0.6830127018922180770, -0.6830127018922204085, -0.2588190451025213501 ) ) ;
#93180=DIRECTION ( 'NONE',  ( 0.7071067811865486830, -0.7071067811865464625, -0.000000000000000000 ) ) ;
#93181=DIRECTION ( 'NONE',  ( 0.7071067811865487940, -0.7071067811865463515, 0.000000000000000000 ) ) ;
#93182=VECTOR ( 'NONE', #65498, 1000.000000000000000 ) ;
#93184=LINE ( 'NONE', #138846, #67802 ) ;
#93185=ORIENTED_EDGE ( 'NONE', *, *, #20349, .F. ) ;
#93186=CARTESIAN_POINT ( 'NONE',  ( -4.499999999999976019, 1.030536316426498233, -5.498701923753791299 ) ) ;
#93187=LINE ( 'NONE', #81628, #92860 ) ;
#93188=ORIENTED_EDGE ( 'NONE', *, *, #100797, .T. ) ;
#93189=ORIENTED_EDGE ( 'NONE', *, *, #120725, .F. ) ;
#93192=ORIENTED_EDGE ( 'NONE', *, *, #33910, .T. ) ;
#93195=VERTEX_POINT ( 'NONE', #61319 ) ;
#93196=FACE_OUTER_BOUND ( 'NONE', #41952, .T. ) ;
#93197=EDGE_LOOP ( 'NONE', ( #12269, #43760, #100378, #63142, #120136 ) ) ;
#93198=FACE_OUTER_BOUND ( 'NONE', #32339, .T. ) ;
#93199=CARTESIAN_POINT ( 'NONE',  ( -29.67183060077626422, 11.25929247661560595, 4.000000000000000000 ) ) ;
#93201=ORIENTED_EDGE ( 'NONE', *, *, #132894, .F. ) ;
#93202=PLANE ( 'NONE',  #28413 ) ;
#93205=ORIENTED_EDGE ( 'NONE', *, *, #122322, .F. ) ;
#93206=DIRECTION ( 'NONE',  ( 0.7071067811865487940, 0.7071067811865463515, -0.000000000000000000 ) ) ;
#93207=ORIENTED_EDGE ( 'NONE', *, *, #86218, .F. ) ;
#93209=ORIENTED_EDGE ( 'NONE', *, *, #85357, .T. ) ;
#93211=ORIENTED_EDGE ( 'NONE', *, *, #83115, .F. ) ;
#93212=VERTEX_POINT ( 'NONE', #4678 ) ;
#93213=CARTESIAN_POINT ( 'NONE',  ( 0.000000000000000000, 0.000000000000000000, 5.000000000000000000 ) ) ;
#93216=LINE ( 'NONE', #82362, #58506 ) ;
#93217=FACE_OUTER_BOUND ( 'NONE', #98712, .T. ) ;
#93218=DIRECTION ( 'NONE',  ( 0.7071067811865487940, 0.7071067811865463515, 0.000000000000000000 ) ) ;
#93219=EDGE_CURVE ( 'NONE', #129026, #76029, #95311, .T. ) ;
#93220=ADVANCED_FACE ( 'NONE', ( #71437 ), #82320, .F. ) ;
#93221=LINE ( 'NONE', #36013, #67415 ) ;
#93222=ORIENTED_EDGE ( 'NONE', *, *, #138465, .T. ) ;
#93224=ADVANCED_FACE ( 'NONE', ( #105457 ), #60591, .F. ) ;
#93225=ADVANCED_FACE ( 'NONE', ( #6122 ), #50400, .F. ) ;
#93227=PLANE ( 'NONE',  #20743 ) ;
#93229=DIRECTION ( 'NONE',  ( 0.7071067811865487940, -0.7071067811865463515, 0.000000000000000000 ) ) ;
#93230=ORIENTED_EDGE ( 'NONE', *, *, #104661, .T. ) ;
#93231=VERTEX_POINT ( 'NONE', #137408 ) ;
#93232=EDGE_CURVE ( 'NONE', #121879, #114032, #134292, .T. ) ;
#93233=ORIENTED_EDGE ( 'NONE', *, *, #136647, .F. ) ;
#93236=CARTESIAN_POINT ( 'NONE',  ( -34.17183060077623225, 9.759292476615625489, 4.000000000000000000 ) ) ;
#93238=EDGE_CURVE ( 'NONE', #79175, #56422, #5427, .T. ) ;
#93239=DIRECTION ( 'NONE',  ( -1.000000000000000000, 0.000000000000000000, -0.000000000000000000 ) ) ;
#93244=DIRECTION ( 'NONE',  ( 0.7071067811865487940, -0.7071067811865463515, -0.000000000000000000 ) ) ;
#93245=LINE ( 'NONE', #47646, #92708 ) ;
#93246=DIRECTION ( 'NONE',  ( -0.7071067811865486830, -0.7071067811865464625, 0.000000000000000000 ) ) ;
#93247=FACE_OUTER_BOUND ( 'NONE', #107670, .T. ) ;
#93249=VECTOR ( 'NONE', #125240, 1000.000000000000227 ) ;
#93250=DIRECTION ( 'NONE',  ( 0.6830127018922180770, -0.6830127018922204085, -0.2588190451025213501 ) ) ;
#93251=ORIENTED_EDGE ( 'NONE', *, *, #65609, .F. ) ;
#93252=EDGE_CURVE ( 'NONE', #10395, #30730, #132266, .T. ) ;
#93254=DIRECTION ( 'NONE',  ( -0.3543493200069162685, -0.000000000000000000, -0.9351131265310288487 ) ) ;
#93255=ORIENTED_EDGE ( 'NONE', *, *, #81991, .T. ) ;
#93256=LINE ( 'NONE', #103396, #85697 ) ;
#93257=CARTESIAN_POINT ( 'NONE',  ( -17.99999999999987566, 9.631307414974306980, -9.079085613539584543 ) ) ;
#93258=VERTEX_POINT ( 'NONE', #131522 ) ;
#93260=VECTOR ( 'NONE', #98462, 1000.000000000000000 ) ;
#93261=EDGE_LOOP ( 'NONE', ( #79936, #129317, #47943, #124807 ) ) ;
#93262=LINE ( 'NONE', #27275, #53678 ) ;
#93263=ORIENTED_EDGE ( 'NONE', *, *, #33201, .F. ) ;
#93264=EDGE_CURVE ( 'NONE', #63012, #8822, #30799, .T. ) ;
#93265=DIRECTION ( 'NONE',  ( 0.7071067811865487940, 0.7071067811865463515, 0.000000000000000000 ) ) ;
#93268=ORIENTED_EDGE ( 'NONE', *, *, #8135, .F. ) ;
#93269=DIRECTION ( 'NONE',  ( 0.7071067811865487940, 0.7071067811865463515, -0.000000000000000000 ) ) ;
#93270=CARTESIAN_POINT ( 'NONE',  ( -34.49999999999976552, 6.054329344830883031, 4.994342998332166772 ) ) ;
#93272=EDGE_CURVE ( 'NONE', #31242, #82671, #108292, .T. ) ;
#93274=VECTOR ( 'NONE', #70469, 999.9999999999998863 ) ;
#93276=ORIENTED_EDGE ( 'NONE', *, *, #80818, .T. ) ;
#93277=VECTOR ( 'NONE', #52382, 1000.000000000000000 ) ;
#93278=VECTOR ( 'NONE', #56144, 1000.000000000000000 ) ;
#93279=DIRECTION ( 'NONE',  ( -0.6830127018922180770, -0.6830127018922204085, -0.2588190451025213501 ) ) ;
#93281=ORIENTED_EDGE ( 'NONE', *, *, #111040, .T. ) ;
#93283=EDGE_CURVE ( 'NONE', #89124, #130861, #31497, .T. ) ;
#93284=LINE ( 'NONE', #27295, #80158 ) ;
#93286=CARTESIAN_POINT ( 'NONE',  ( 45.29974487139158867, -27.71228299555237840, 4.000000000000000000 ) ) ;
#93289=ORIENTED_EDGE ( 'NONE', *, *, #53280, .F. ) ;
#93290=DIRECTION ( 'NONE',  ( -0.7071067811865486830, -0.7071067811865464625, -0.000000000000000000 ) ) ;
#93291=EDGE_CURVE ( 'NONE', #118704, #122228, #65591, .T. ) ;
#93292=ADVANCED_FACE ( 'NONE', ( #141693 ), #130102, .F. ) ;
#93294=CARTESIAN_POINT ( 'NONE',  ( 11.99999999999992006, -7.447814304570750998, 5.000000000000000000 ) ) ;
#93295=CARTESIAN_POINT ( 'NONE',  ( 3.328169399223507519, 2.259292476615690770, 4.000000000000000000 ) ) ;
#93296=CARTESIAN_POINT ( 'NONE',  ( 0.000000000000000000, 0.000000000000000000, 5.000000000000000000 ) ) ;
#93297=ORIENTED_EDGE ( 'NONE', *, *, #44094, .T. ) ;
#93299=CARTESIAN_POINT ( 'NONE',  ( -22.89835756248665888, 7.738675393078206177, 4.667276354320995857 ) ) ;
#93302=ORIENTED_EDGE ( 'NONE', *, *, #37347, .T. ) ;
#93304=ORIENTED_EDGE ( 'NONE', *, *, #92394, .F. ) ;
#93307=ORIENTED_EDGE ( 'NONE', *, *, #56795, .F. ) ;
#93308=EDGE_CURVE ( 'NONE', #110817, #103815, #77173, .T. ) ;
#93310=DIRECTION ( 'NONE',  ( -0.7071067811865486830, -0.7071067811865464625, 0.000000000000000000 ) ) ;
#93312=LINE ( 'NONE', #107030, #105921 ) ;
#93313=VERTEX_POINT ( 'NONE', #121343 ) ;
#93315=CARTESIAN_POINT ( 'NONE',  ( -2.816011393730999401, 28.73617430169785436, 5.000000000000000000 ) ) ;
#93317=VERTEX_POINT ( 'NONE', #66278 ) ;
#93318=EDGE_CURVE ( 'NONE', #84223, #132339, #87306, .T. ) ;
#93319=VECTOR ( 'NONE', #15446, 1000.000000000000000 ) ;
#93320=DIRECTION ( 'NONE',  ( -0.7071067811865486830, -0.7071067811865464625, 0.000000000000000000 ) ) ;
#93321=CARTESIAN_POINT ( 'NONE',  ( -16.17183060077635659, 18.75929247661552424, 4.000000000000000000 ) ) ;
#93322=LINE ( 'NONE', #17866, #28489 ) ;
#93323=ORIENTED_EDGE ( 'NONE', *, *, #129937, .T. ) ;
#93324=ORIENTED_EDGE ( 'NONE', *, *, #128213, .F. ) ;
#93325=EDGE_CURVE ( 'NONE', #112402, #4116, #42396, .T. ) ;
#93326=CARTESIAN_POINT ( 'NONE',  ( -29.67183060077626422, 8.259292476615639700, 4.000000000000000000 ) ) ;
#93328=DIRECTION ( 'NONE',  ( -0.7071067811865486830, -0.7071067811865464625, 0.000000000000000000 ) ) ;
#93329=DIRECTION ( 'NONE',  ( 0.7071067811865487940, 0.7071067811865463515, 0.000000000000000000 ) ) ;
#93334=FACE_OUTER_BOUND ( 'NONE', #55523, .T. ) ;
#93337=VECTOR ( 'NONE', #14054, 1000.000000000000000 ) ;
#93338=ORIENTED_EDGE ( 'NONE', *, *, #38670, .T. ) ;
#93339=( BOUNDED_CURVE ( )  B_SPLINE_CURVE ( 3, ( #121532, #77369, #130303, #76643 ),
 .UNSPECIFIED., .F., .T. ) 
 B_SPLINE_CURVE_WITH_KNOTS ( ( 4, 4 ),
 ( 1.964434688349479652, 3.503810798801452187 ),
 .UNSPECIFIED. ) 
 CURVE ( )  GEOMETRIC_REPRESENTATION_ITEM ( )  RATIONAL_B_SPLINE_CURVE ( ( 1.000000000000000000, 0.8120851936182260644, 0.8120851936182260644, 1.000000000000000000 ) ) 
 REPRESENTATION_ITEM ( '' )  );
#93340=ORIENTED_EDGE ( 'NONE', *, *, #94807, .F. ) ;
#93342=AXIS2_PLACEMENT_3D ( 'NONE', #49639, #36574, #71366 ) ;
#93343=ADVANCED_FACE ( 'NONE', ( #110449 ), #96704, .F. ) ;
#93344=PLANE ( 'NONE',  #26970 ) ;
#93346=EDGE_CURVE ( 'NONE', #41198, #18669, #75027, .T. ) ;
#93347=ORIENTED_EDGE ( 'NONE', *, *, #65026, .T. ) ;
#93350=PLANE ( 'NONE',  #52603 ) ;
#93351=DIRECTION ( 'NONE',  ( 0.7071067811865486830, -0.7071067811865464625, -0.000000000000000000 ) ) ;
#93353=DIRECTION ( 'NONE',  ( 0.7071067811865487940, 0.7071067811865463515, 0.000000000000000000 ) ) ;
#93354=ORIENTED_EDGE ( 'NONE', *, *, #34335, .F. ) ;
#93356=CARTESIAN_POINT ( 'NONE',  ( -19.69064382391260892, -2.759520746520534473, 4.000000000000000000 ) ) ;
#93358=DIRECTION ( 'NONE',  ( -0.7071067811865486830, 0.7071067811865464625, 0.000000000000000000 ) ) ;
#93359=ORIENTED_EDGE ( 'NONE', *, *, #53076, .T. ) ;
#93360=ADVANCED_FACE ( 'NONE', ( #143106 ), #75719, .F. ) ;
#93361=VERTEX_POINT ( 'NONE', #142413 ) ;
#93362=CARTESIAN_POINT ( 'NONE',  ( -6.489213562373093325, -27.52281430457059841, 5.000000000000000000 ) ) ;
#93363=ORIENTED_EDGE ( 'NONE', *, *, #121089, .F. ) ;
#93365=AXIS2_PLACEMENT_3D ( 'NONE', #67857, #57678, #122906 ) ;
#93368=CARTESIAN_POINT ( 'NONE',  ( 60.29974487139158867, -27.71228299555248142, 4.000000000000000000 ) ) ;
#93369=CARTESIAN_POINT ( 'NONE',  ( -31.88982677111766506, -22.22500000000000142, 4.785647885939354751 ) ) ;
#93371=DIRECTION ( 'NONE',  ( -0.6830127018922181881, 0.6830127018922202975, -0.2588190451025214056 ) ) ;
#93372=LINE ( 'NONE', #91263, #1932 ) ;
#93373=FACE_OUTER_BOUND ( 'NONE', #50781, .T. ) ;
#93374=VECTOR ( 'NONE', #56570, 999.9999999999998863 ) ;
#93375=CARTESIAN_POINT ( 'NONE',  ( -23.67183060077630685, -15.74070752338411339, 4.000000000000000000 ) ) ;
#93376=FACE_OUTER_BOUND ( 'NONE', #72981, .T. ) ;
#93377=VECTOR ( 'NONE', #87672, 1000.000000000000000 ) ;
#93379=CARTESIAN_POINT ( 'NONE',  ( -27.79289321881325492, 0.7592924766157086447, 5.000000000000000000 ) ) ;
#93380=VERTEX_POINT ( 'NONE', #140259 ) ;
#93381=CARTESIAN_POINT ( 'NONE',  ( 63.48921356237309510, -27.52281430457099631, 5.000000000000000000 ) ) ;
#93382=ORIENTED_EDGE ( 'NONE', *, *, #55169, .F. ) ;
#93383=ORIENTED_EDGE ( 'NONE', *, *, #46662, .T. ) ;
#93386=VERTEX_POINT ( 'NONE', #85864 ) ;
#93387=DIRECTION ( 'NONE',  ( 1.000000000000000000, 0.000000000000000000, 0.000000000000000000 ) ) ;
#93388=CARTESIAN_POINT ( 'NONE',  ( -0.8518164496185489654, 17.25929247661554200, 8.802941693769200882 ) ) ;
#93389=CARTESIAN_POINT ( 'NONE',  ( 0.000000000000000000, 0.000000000000000000, 5.000000000000000000 ) ) ;
#93390=CARTESIAN_POINT ( 'NONE',  ( 31.17183060077625001, 9.759292476615625489, 4.000000000000000000 ) ) ;
#93391=EDGE_CURVE ( 'NONE', #120276, #52005, #43100, .T. ) ;
#93392=ORIENTED_EDGE ( 'NONE', *, *, #109562, .T. ) ;
#93394=ORIENTED_EDGE ( 'NONE', *, *, #89284, .F. ) ;
#93395=CARTESIAN_POINT ( 'NONE',  ( -8.999999999999944933, 4.965500833774321165, -4.007596771432636373 ) ) ;
#93396=EDGE_CURVE ( 'NONE', #66330, #60758, #109031, .T. ) ;
#93397=EDGE_CURVE ( 'NONE', #55705, #137664, #63445, .T. ) ;
#93398=VECTOR ( 'NONE', #33396, 1000.000000000000227 ) ;
#93400=CARTESIAN_POINT ( 'NONE',  ( 14.51078643762690490, -27.52281430457045275, 5.000000000000000000 ) ) ;
#93401=EDGE_CURVE ( 'NONE', #52621, #137809, #13994, .T. ) ;
#93402=CARTESIAN_POINT ( 'NONE',  ( 30.32816939922332011, 5.259292476615665457, 4.000000000000000000 ) ) ;
#93403=CARTESIAN_POINT ( 'NONE',  ( 6.489213562373093325, -27.52281430457059841, 5.000000000000000000 ) ) ;
#93404=ORIENTED_EDGE ( 'NONE', *, *, #97551, .F. ) ;
#93405=ORIENTED_EDGE ( 'NONE', *, *, #14510, .F. ) ;
#93407=ORIENTED_EDGE ( 'NONE', *, *, #4452, .T. ) ;
#93409=DIRECTION ( 'NONE',  ( -0.000000000000000000, 0.3543493200069153248, 0.9351131265310292928 ) ) ;
#93410=LINE ( 'NONE', #2819, #86730 ) ;
#93411=ADVANCED_FACE ( 'NONE', ( #80728 ), #11853, .T. ) ;
#93412=PLANE ( 'NONE',  #65828 ) ;
#93415=LINE ( 'NONE', #27418, #108215 ) ;
#93416=ADVANCED_FACE ( 'NONE', ( #45264 ), #980, .T. ) ;
#93417=CARTESIAN_POINT ( 'NONE',  ( -22.00193056682082471, -22.22500000000000142, 4.500000000000000888 ) ) ;
#93419=LINE ( 'NONE', #37628, #118312 ) ;
#93420=CARTESIAN_POINT ( 'NONE',  ( 51.48921356237309510, -27.52281430457091460, 5.000000000000000000 ) ) ;
#93421=ORIENTED_EDGE ( 'NONE', *, *, #139606, .F. ) ;
#93422=DIRECTION ( 'NONE',  ( -0.000000000000000000, 0.000000000000000000, 1.000000000000000000 ) ) ;
#93423=ORIENTED_EDGE ( 'NONE', *, *, #73607, .F. ) ;
#93424=VECTOR ( 'NONE', #94629, 1000.000000000000000 ) ;
#93425=EDGE_CURVE ( 'NONE', #97256, #56540, #25593, .T. ) ;
#93426=LINE ( 'NONE', #100904, #41269 ) ;
#93428=ORIENTED_EDGE ( 'NONE', *, *, #51267, .F. ) ;
#93429=ORIENTED_EDGE ( 'NONE', *, *, #86948, .T. ) ;
#93430=EDGE_CURVE ( 'NONE', #64028, #140629, #56142, .T. ) ;
#93432=DIRECTION ( 'NONE',  ( -0.7071067811865487940, 0.7071067811865463515, -0.000000000000000000 ) ) ;
#93433=DIRECTION ( 'NONE',  ( -0.7071067811865486830, -0.7071067811865464625, 0.000000000000000000 ) ) ;
#93436=ORIENTED_EDGE ( 'NONE', *, *, #19232, .T. ) ;
#93438=VECTOR ( 'NONE', #24347, 999.9999999999998863 ) ;
#93439=LINE ( 'NONE', #50642, #1181 ) ;
#93440=PLANE ( 'NONE',  #101842 ) ;
#93442=FACE_OUTER_BOUND ( 'NONE', #109466, .T. ) ;
#93444=LINE ( 'NONE', #39058, #32396 ) ;
#93445=CARTESIAN_POINT ( 'NONE',  ( -2.510786437626908008, -27.52281430457053446, 5.000000000000000000 ) ) ;
#93447=CARTESIAN_POINT ( 'NONE',  ( 53.99451991528749062, 28.92564299267975869, 4.000000000000000000 ) ) ;
#93450=AXIS2_PLACEMENT_3D ( 'NONE', #89039, #57137, #2700 ) ;
#93452=DIRECTION ( 'NONE',  ( 0.7071067811865486830, -0.7071067811865464625, -0.000000000000000000 ) ) ;
#93453=FACE_OUTER_BOUND ( 'NONE', #111932, .T. ) ;
#93454=EDGE_LOOP ( 'NONE', ( #80601, #40517, #20910, #39502 ) ) ;
#93455=ORIENTED_EDGE ( 'NONE', *, *, #46116, .T. ) ;
#93457=ORIENTED_EDGE ( 'NONE', *, *, #41523, .T. ) ;
#93458=VERTEX_POINT ( 'NONE', #66985 ) ;
#93459=EDGE_CURVE ( 'NONE', #139774, #37807, #135804, .T. ) ;
#93461=DIRECTION ( 'NONE',  ( -0.3543493200069162685, -0.000000000000000000, -0.9351131265310288487 ) ) ;
#93462=VECTOR ( 'NONE', #39574, 1000.000000000000000 ) ;
#93463=LINE ( 'NONE', #17993, #43151 ) ;
#93464=ORIENTED_EDGE ( 'NONE', *, *, #29763, .F. ) ;
#93465=LINE ( 'NONE', #39829, #16198 ) ;
#93467=LINE ( 'NONE', #62279, #127445 ) ;
#93469=PLANE ( 'NONE',  #12306 ) ;
#93470=DIRECTION ( 'NONE',  ( 0.6830127018922181881, 0.6830127018922202975, -0.2588190451025214056 ) ) ;
#93471=VECTOR ( 'NONE', #53182, 1000.000000000000000 ) ;
#93472=FACE_OUTER_BOUND ( 'NONE', #15638, .T. ) ;
#93473=CARTESIAN_POINT ( 'NONE',  ( -14.81601139373099585, 28.73617430169776910, 5.000000000000000000 ) ) ;
#93474=DIRECTION ( 'NONE',  ( 0.7071067811865487940, 0.7071067811865463515, 0.000000000000000000 ) ) ;
#93475=DIRECTION ( 'NONE',  ( -0.6830127018922180770, 0.6830127018922202975, -0.2588190451025213501 ) ) ;
#93477=EDGE_CURVE ( 'NONE', #121112, #687, #107588, .T. ) ;
#93478=DIRECTION ( 'NONE',  ( 0.7071067811865487940, 0.7071067811865463515, -0.000000000000000000 ) ) ;
#93479=VERTEX_POINT ( 'NONE', #57551 ) ;
#93480=ORIENTED_EDGE ( 'NONE', *, *, #16107, .T. ) ;
#93483=ORIENTED_EDGE ( 'NONE', *, *, #111853, .T. ) ;
#93485=DIRECTION ( 'NONE',  ( 0.7071067811865486830, -0.7071067811865464625, -0.000000000000000000 ) ) ;
#93486=CARTESIAN_POINT ( 'NONE',  ( 30.79289321881324781, -11.24070752338416668, 5.000000000000000000 ) ) ;
#93487=ORIENTED_EDGE ( 'NONE', *, *, #127688, .T. ) ;
#93488=CARTESIAN_POINT ( 'NONE',  ( 14.09068777029287567, 6.496774105546209377, 4.000000000000000000 ) ) ;
#93489=CARTESIAN_POINT ( 'NONE',  ( -2.671830600776449405, -0.7407075233842770334, 4.000000000000000000 ) ) ;
#93490=VECTOR ( 'NONE', #135450, 999.9999999999998863 ) ;
#93492=VERTEX_POINT ( 'NONE', #127050 ) ;
#93493=ADVANCED_FACE ( 'NONE', ( #84307 ), #15406, .T. ) ;
#93494=DIRECTION ( 'NONE',  ( 1.000000000000000000, 0.000000000000000000, 0.000000000000000000 ) ) ;
#93495=ORIENTED_EDGE ( 'NONE', *, *, #88681, .F. ) ;
#93496=CARTESIAN_POINT ( 'NONE',  ( 16.49999999999988276, -16.53360074219757081, 5.000000000000000000 ) ) ;
#93497=FACE_OUTER_BOUND ( 'NONE', #97658, .T. ) ;
#93498=ORIENTED_EDGE ( 'NONE', *, *, #47396, .F. ) ;
#93499=ORIENTED_EDGE ( 'NONE', *, *, #141453, .F. ) ;
#93500=ADVANCED_FACE ( 'NONE', ( #48805 ), #28483, .T. ) ;
#93501=EDGE_LOOP ( 'NONE', ( #23137, #141105, #135789, #87595 ) ) ;
#93502=CARTESIAN_POINT ( 'NONE',  ( -51.18398860626899705, 28.73617430169823095, 5.000000000000000000 ) ) ;
#93503=DIRECTION ( 'NONE',  ( 0.7071067811865487940, 0.7071067811865463515, 0.000000000000000000 ) ) ;
#93505=AXIS2_PLACEMENT_3D ( 'NONE', #141125, #85311, #19363 ) ;
#93507=VECTOR ( 'NONE', #106802, 1000.000000000000000 ) ;
#93508=CARTESIAN_POINT ( 'NONE',  ( 29.99999999999979039, -7.447814304570749222, 5.000000000000000000 ) ) ;
#93509=ORIENTED_EDGE ( 'NONE', *, *, #103001, .T. ) ;
#93510=ORIENTED_EDGE ( 'NONE', *, *, #102837, .T. ) ;
#93511=PLANE ( 'NONE',  #108084 ) ;
#93512=ORIENTED_EDGE ( 'NONE', *, *, #68300, .T. ) ;
#93513=ORIENTED_EDGE ( 'NONE', *, *, #98621, .F. ) ;
#93514=AXIS2_PLACEMENT_3D ( 'NONE', #44399, #58141, #23297 ) ;
#93515=PLANE ( 'NONE',  #23984 ) ;
#93516=DIRECTION ( 'NONE',  ( -0.7071067811865486830, -0.7071067811865464625, 0.000000000000000000 ) ) ;
#93517=DIRECTION ( 'NONE',  ( -0.7071067811865486830, -0.7071067811865464625, 0.000000000000000000 ) ) ;
#93518=EDGE_CURVE ( 'NONE', #13228, #76266, #139404, .T. ) ;
#93520=VECTOR ( 'NONE', #29732, 1000.000000000000227 ) ;
#93521=DIRECTION ( 'NONE',  ( 0.7071067811865486830, -0.7071067811865464625, -0.000000000000000000 ) ) ;
#93522=LINE ( 'NONE', #128992, #110323 ) ;
#93523=CARTESIAN_POINT ( 'NONE',  ( -24.48921356237309510, -27.52281430457072631, 5.000000000000000000 ) ) ;
#93525=ORIENTED_EDGE ( 'NONE', *, *, #45079, .F. ) ;
#93526=AXIS2_PLACEMENT_3D ( 'NONE', #125709, #26388, #15453 ) ;
#93527=CARTESIAN_POINT ( 'NONE',  ( 18.48921356237309510, -27.52281430457068367, 5.000000000000000000 ) ) ;
#93528=FACE_BOUND ( 'NONE', #110123, .T. ) ;
#93532=DIRECTION ( 'NONE',  ( 0.7071067811865486830, -0.7071067811865464625, -0.000000000000000000 ) ) ;
#93533=CARTESIAN_POINT ( 'NONE',  ( 20.51078643762690490, -27.52281430457041012, 5.000000000000000000 ) ) ;
#93534=EDGE_CURVE ( 'NONE', #106612, #75123, #137237, .T. ) ;
#93536=DIRECTION ( 'NONE',  ( -0.7071067811865486830, -0.7071067811865464625, -0.000000000000000000 ) ) ;
#93537=VERTEX_POINT ( 'NONE', #104594 ) ;
#93538=EDGE_LOOP ( 'NONE', ( #852, #122714, #27316, #23349 ) ) ;
#93539=ORIENTED_EDGE ( 'NONE', *, *, #108630, .T. ) ;
#93540=VECTOR ( 'NONE', #28293, 1000.000000000000227 ) ;
#93542=AXIS2_PLACEMENT_3D ( 'NONE', #135833, #77201, #66310 ) ;
#93543=ORIENTED_EDGE ( 'NONE', *, *, #107966, .F. ) ;
#93544=CARTESIAN_POINT ( 'NONE',  ( 7.828169399223474656, -8.240707523384203981, 4.000000000000000000 ) ) ;
#93545=FACE_OUTER_BOUND ( 'NONE', #91249, .T. ) ;
#93546=CARTESIAN_POINT ( 'NONE',  ( 25.49999999999982947, 1.466399257802255329, 5.000000000000000000 ) ) ;
#93548=LINE ( 'NONE', #91417, #106986 ) ;
#93549=CARTESIAN_POINT ( 'NONE',  ( 75.18398860626899705, 28.73617430169839793, 5.000000000000000000 ) ) ;
#93550=AXIS2_PLACEMENT_3D ( 'NONE', #138199, #61397, #48330 ) ;
#93551=ADVANCED_FACE ( 'NONE', ( #59011 ), #48091, .T. ) ;
#93552=PLANE ( 'NONE',  #60762 ) ;
#93553=LINE ( 'NONE', #37021, #24772 ) ;
#93554=FACE_OUTER_BOUND ( 'NONE', #17505, .T. ) ;
#93555=DIRECTION ( 'NONE',  ( 0.7071067811865487940, 0.7071067811865463515, 0.000000000000000000 ) ) ;
#93557=EDGE_LOOP ( 'NONE', ( #42744, #11512, #108779, #51406 ) ) ;
#93558=ORIENTED_EDGE ( 'NONE', *, *, #22995, .F. ) ;
#93559=VECTOR ( 'NONE', #88434, 1000.000000000000000 ) ;
#93560=ORIENTED_EDGE ( 'NONE', *, *, #135461, .T. ) ;
#93561=ORIENTED_EDGE ( 'NONE', *, *, #20313, .T. ) ;
#93562=FACE_OUTER_BOUND ( 'NONE', #51580, .T. ) ;
#93563=ORIENTED_EDGE ( 'NONE', *, *, #68229, .F. ) ;
#93564=ADVANCED_FACE ( 'NONE', ( #93010 ), #136500, .F. ) ;
#93565=ORIENTED_EDGE ( 'NONE', *, *, #24988, .T. ) ;
#93566=PLANE ( 'NONE',  #63035 ) ;
#93567=CARTESIAN_POINT ( 'NONE',  ( 81.29974487139159578, -27.71228299555262709, 4.000000000000000000 ) ) ;
#93568=CARTESIAN_POINT ( 'NONE',  ( -6.005480084712508493, 28.92564299267933947, 4.000000000000000000 ) ) ;
#93569=VERTEX_POINT ( 'NONE', #70589 ) ;
#93570=DIRECTION ( 'NONE',  ( -0.7071067811865486830, 0.7071067811865464625, 0.000000000000000000 ) ) ;
#93572=CARTESIAN_POINT ( 'NONE',  ( 56.99451991528749062, 28.92564299267978001, 4.000000000000000000 ) ) ;
#93573=DIRECTION ( 'NONE',  ( 0.7071067811865486830, -0.7071067811865464625, -0.000000000000000000 ) ) ;
#93574=EDGE_CURVE ( 'NONE', #106170, #96928, #39363, .T. ) ;
#93576=ORIENTED_EDGE ( 'NONE', *, *, #98516, .T. ) ;
#93578=DIRECTION ( 'NONE',  ( -0.000000000000000000, 0.3543493200069153248, 0.9351131265310292928 ) ) ;
#93579=EDGE_CURVE ( 'NONE', #2946, #81677, #13, .T. ) ;
#93583=ORIENTED_EDGE ( 'NONE', *, *, #22202, .T. ) ;
#93584=EDGE_CURVE ( 'NONE', #25077, #122713, #81451, .T. ) ;
#93585=CARTESIAN_POINT ( 'NONE',  ( 48.18398860626899705, 28.73617430169820608, 5.000000000000000000 ) ) ;
#93586=ORIENTED_EDGE ( 'NONE', *, *, #129540, .F. ) ;
#93587=CARTESIAN_POINT ( 'NONE',  ( 57.18398860626899705, 28.73617430169827358, 5.000000000000000000 ) ) ;
#93588=CARTESIAN_POINT ( 'NONE',  ( 68.99451991528748351, 28.92564299267986172, 4.000000000000000000 ) ) ;
#93589=CARTESIAN_POINT ( 'NONE',  ( 75.18398860626899705, 28.73617430169839793, 5.000000000000000000 ) ) ;
#93590=DIRECTION ( 'NONE',  ( -0.6830127018922180770, 0.6830127018922202975, -0.2588190451025213501 ) ) ;
#93592=EDGE_CURVE ( 'NONE', #116079, #104350, #26333, .T. ) ;
#93594=VECTOR ( 'NONE', #93720, 1000.000000000000000 ) ;
#93595=VERTEX_POINT ( 'NONE', #105302 ) ;
#93596=DIRECTION ( 'NONE',  ( 0.7071067811865486830, -0.7071067811865464625, -0.000000000000000000 ) ) ;
#93597=CARTESIAN_POINT ( 'NONE',  ( 27.70710678118635428, 8.259292476615634371, 5.000000000000000000 ) ) ;
#93598=DIRECTION ( 'NONE',  ( 0.6830127018922181881, 0.6830127018922202975, -0.2588190451025214056 ) ) ;
#93599=EDGE_LOOP ( 'NONE', ( #114030, #49581, #1944, #104947, #89065 ) ) ;
#93600=CARTESIAN_POINT ( 'NONE',  ( 81.18398860626899705, 28.73617430169844056, 5.000000000000000000 ) ) ;
#93602=VERTEX_POINT ( 'NONE', #5958 ) ;
#93603=EDGE_CURVE ( 'NONE', #138830, #46125, #127944, .T. ) ;
#93604=CARTESIAN_POINT ( 'NONE',  ( 10.25398840412855606, 22.22500000000000142, -12.12000758559782554 ) ) ;
#93605=ORIENTED_EDGE ( 'NONE', *, *, #83958, .T. ) ;
#93606=EDGE_CURVE ( 'NONE', #90217, #87653, #72743, .T. ) ;
#93608=CARTESIAN_POINT ( 'NONE',  ( 33.18398860626899705, 28.73617430169810305, 5.000000000000000000 ) ) ;
#93611=ORIENTED_EDGE ( 'NONE', *, *, #142481, .T. ) ;
#93612=CARTESIAN_POINT ( 'NONE',  ( 28.49999999999981171, -4.216083040037226226, -7.486842126848721968 ) ) ;
#93613=EDGE_CURVE ( 'NONE', #5098, #115334, #54522, .T. ) ;
#93615=AXIS2_PLACEMENT_3D ( 'NONE', #54258, #142661, #22977 ) ;
#93616=ORIENTED_EDGE ( 'NONE', *, *, #99976, .F. ) ;
#93617=CARTESIAN_POINT ( 'NONE',  ( -7.171830600776418763, 18.75929247661553489, 4.000000000000000000 ) ) ;
#93618=VECTOR ( 'NONE', #24274, 1000.000000000000227 ) ;
#93620=LINE ( 'NONE', #80097, #60404 ) ;
#93621=LINE ( 'NONE', #105195, #74535 ) ;
#93622=EDGE_CURVE ( 'NONE', #66621, #22720, #129919, .T. ) ;
#93624=LINE ( 'NONE', #118189, #127055 ) ;
#93626=CARTESIAN_POINT ( 'NONE',  ( 16.83455439249994612, 8.717631302929021331, 5.000000000000000000 ) ) ;
#93627=ORIENTED_EDGE ( 'NONE', *, *, #114262, .T. ) ;
#93629=ORIENTED_EDGE ( 'NONE', *, *, #14210, .T. ) ;
#93631=VERTEX_POINT ( 'NONE', #30626 ) ;
#93634=ORIENTED_EDGE ( 'NONE', *, *, #1847, .F. ) ;
#93635=EDGE_CURVE ( 'NONE', #99005, #37562, #85680, .T. ) ;
#93637=DIRECTION ( 'NONE',  ( -0.7071067811865486830, -0.7071067811865464625, -0.000000000000000000 ) ) ;
#93638=ORIENTED_EDGE ( 'NONE', *, *, #18175, .T. ) ;
#93639=( BOUNDED_CURVE ( )  B_SPLINE_CURVE ( 3, ( #118861, #19549, #42764, #29008 ),
 .UNSPECIFIED., .F., .T. ) 
 B_SPLINE_CURVE_WITH_KNOTS ( ( 4, 4 ),
 ( 1.864375635226942718, 1.933014472006551188 ),
 .UNSPECIFIED. ) 
 CURVE ( )  GEOMETRIC_REPRESENTATION_ITEM ( )  RATIONAL_B_SPLINE_CURVE ( ( 1.000000000000000000, 0.9996074310407765395, 0.9996074310407765395, 1.000000000000000000 ) ) 
 REPRESENTATION_ITEM ( '' )  );
#93640=DIRECTION ( 'NONE',  ( 0.7071067811865487940, 0.7071067811865463515, 0.000000000000000000 ) ) ;
#93641=PLANE ( 'NONE',  #94980 ) ;
#93643=AXIS2_PLACEMENT_3D ( 'NONE', #140636, #129768, #30470 ) ;
#93644=DIRECTION ( 'NONE',  ( -0.000000000000000000, 0.3543493200069153248, 0.9351131265310292928 ) ) ;
#93646=ORIENTED_EDGE ( 'NONE', *, *, #131093, .T. ) ;
#93647=LINE ( 'NONE', #127710, #81241 ) ;
#93649=DIRECTION ( 'NONE',  ( -0.000000000000000000, 0.000000000000000000, 1.000000000000000000 ) ) ;
#93652=CARTESIAN_POINT ( 'NONE',  ( -2.999999999999981792, 18.08204922493372635, 0.9627537363044941232 ) ) ;
#93654=AXIS2_PLACEMENT_3D ( 'NONE', #20791, #97642, #98375 ) ;
#93656=EDGE_CURVE ( 'NONE', #86264, #23390, #74857, .T. ) ;
#93657=DIRECTION ( 'NONE',  ( 0.7071067811865487940, 0.7071067811865463515, -0.000000000000000000 ) ) ;
#93660=ORIENTED_EDGE ( 'NONE', *, *, #108980, .T. ) ;
#93661=ORIENTED_EDGE ( 'NONE', *, *, #55183, .F. ) ;
#93662=AXIS2_PLACEMENT_3D ( 'NONE', #90199, #121394, #135173 ) ;
#93664=EDGE_LOOP ( 'NONE', ( #141678, #10505, #8815, #103661 ) ) ;
#93665=CARTESIAN_POINT ( 'NONE',  ( 4.499999999999979572, -14.94781430457068083, 5.000000000000000000 ) ) ;
#93666=LINE ( 'NONE', #126977, #84879 ) ;
#93667=ORIENTED_EDGE ( 'NONE', *, *, #77692, .F. ) ;
#93669=LINE ( 'NONE', #27673, #16534 ) ;
#93670=LINE ( 'NONE', #50169, #76663 ) ;
#93671=VECTOR ( 'NONE', #93180, 1000.000000000000000 ) ;
#93673=ORIENTED_EDGE ( 'NONE', *, *, #86571, .T. ) ;
#93674=EDGE_CURVE ( 'NONE', #29516, #445, #140771, .T. ) ;
#93675=CARTESIAN_POINT ( 'NONE',  ( 11.20710678118646619, 6.759292476615645029, 5.000000000000000000 ) ) ;
#93676=ORIENTED_EDGE ( 'NONE', *, *, #33946, .F. ) ;
#93677=CARTESIAN_POINT ( 'NONE',  ( -18.48921356237309510, -27.52281430457068367, 5.000000000000000000 ) ) ;
#93679=CARTESIAN_POINT ( 'NONE',  ( 63.48921356237309510, -27.52281430457099631, 5.000000000000000000 ) ) ;
#93680=VERTEX_POINT ( 'NONE', #119033 ) ;
#93682=ADVANCED_FACE ( 'NONE', ( #98010 ), #19716, .F. ) ;
#93683=VERTEX_POINT ( 'NONE', #108128 ) ;
#93684=CARTESIAN_POINT ( 'NONE',  ( 18.48921356237309510, -27.52281430457068367, 5.000000000000000000 ) ) ;
#93685=DIRECTION ( 'NONE',  ( 0.6830127018922181881, 0.6830127018922202975, -0.2588190451025214056 ) ) ;
#93689=VERTEX_POINT ( 'NONE', #129185 ) ;
#93690=DIRECTION ( 'NONE',  ( 1.000000000000000000, 0.000000000000000000, 0.000000000000000000 ) ) ;
#93691=DIRECTION ( 'NONE',  ( -0.7071067811865486830, 0.7071067811865464625, 0.000000000000000000 ) ) ;
#93692=ORIENTED_EDGE ( 'NONE', *, *, #39811, .F. ) ;
#93694=DIRECTION ( 'NONE',  ( 1.000000000000000000, 0.000000000000000000, 0.000000000000000000 ) ) ;
#93695=VERTEX_POINT ( 'NONE', #76262 ) ;
#93699=ADVANCED_FACE ( 'NONE', ( #106708 ), #42931, .F. ) ;
#93700=VERTEX_POINT ( 'NONE', #64666 ) ;
#93701=CARTESIAN_POINT ( 'NONE',  ( -19.49999999999985789, -19.53360074219754239, 5.000000000000000000 ) ) ;
#93703=ADVANCED_FACE ( 'NONE', ( #118306 ), #87838, .T. ) ;
#93704=FACE_BOUND ( 'NONE', #38260, .T. ) ;
#93705=FACE_OUTER_BOUND ( 'NONE', #83892, .T. ) ;
#93706=LINE ( 'NONE', #114713, #123217 ) ;
#93707=CARTESIAN_POINT ( 'NONE',  ( -8.999999999999936051, -13.97847968911261241, -0.1324546996127008436 ) ) ;
#93709=ORIENTED_EDGE ( 'NONE', *, *, #115627, .T. ) ;
#93710=CARTESIAN_POINT ( 'NONE',  ( -23.29289321881329755, 8.259292476615625489, 5.000000000000000000 ) ) ;
#93712=ORIENTED_EDGE ( 'NONE', *, *, #43145, .T. ) ;
#93713=DIRECTION ( 'NONE',  ( -0.7071067811865486830, 0.7071067811865464625, 0.000000000000000000 ) ) ;
#93714=ORIENTED_EDGE ( 'NONE', *, *, #131769, .T. ) ;
#93715=VERTEX_POINT ( 'NONE', #8107 ) ;
#93719=AXIS2_PLACEMENT_3D ( 'NONE', #50317, #116275, #8872 ) ;
#93720=DIRECTION ( 'NONE',  ( 0.7071067811865487940, 0.7071067811865463515, -0.000000000000000000 ) ) ;
#93721=ORIENTED_EDGE ( 'NONE', *, *, #128352, .T. ) ;
#93722=DIRECTION ( 'NONE',  ( -0.6830127018922180770, -0.6830127018922204085, -0.2588190451025214056 ) ) ;
#93723=ADVANCED_FACE ( 'NONE', ( #73411 ), #18261, .F. ) ;
#93724=DIRECTION ( 'NONE',  ( -1.000000000000000000, 0.000000000000000000, 0.000000000000000000 ) ) ;
#93726=DIRECTION ( 'NONE',  ( -0.000000000000000000, 0.000000000000000000, 1.000000000000000000 ) ) ;
#93727=DIRECTION ( 'NONE',  ( -0.3543493200069162685, -0.000000000000000000, -0.9351131265310288487 ) ) ;
#93728=CARTESIAN_POINT ( 'NONE',  ( 0.000000000000000000, 0.000000000000000000, 5.000000000000000000 ) ) ;
#93729=ORIENTED_EDGE ( 'NONE', *, *, #138997, .F. ) ;
#93730=VERTEX_POINT ( 'NONE', #24716 ) ;
#93732=DIRECTION ( 'NONE',  ( -0.6830127018922181881, 0.6830127018922202975, -0.2588190451025214056 ) ) ;
#93733=EDGE_LOOP ( 'NONE', ( #83509, #122757, #114180, #140879 ) ) ;
#93734=EDGE_LOOP ( 'NONE', ( #117133, #9396, #60237, #57054 ) ) ;
#93735=ORIENTED_EDGE ( 'NONE', *, *, #10804, .T. ) ;
#93736=CARTESIAN_POINT ( 'NONE',  ( -5.999999999999960032, 10.21212019023808004, -2.019456568337786972 ) ) ;
#93741=DIRECTION ( 'NONE',  ( -0.7071067811865486830, -0.7071067811865464625, 0.000000000000000000 ) ) ;
#93742=VECTOR ( 'NONE', #89460, 1000.000000000000000 ) ;
#93745=EDGE_CURVE ( 'NONE', #126076, #88152, #88576, .T. ) ;
#93746=CARTESIAN_POINT ( 'NONE',  ( 24.18398860626899705, 28.73617430169804265, 5.000000000000000000 ) ) ;
#93747=EDGE_LOOP ( 'NONE', ( #20154, #13475, #98304, #42976 ) ) ;
#93748=VECTOR ( 'NONE', #79674, 999.9999999999998863 ) ;
#93749=CARTESIAN_POINT ( 'NONE',  ( 6.411614905948259668, 22.22500000000000142, 4.777194822843816802 ) ) ;
#93750=EDGE_CURVE ( 'NONE', #32455, #41056, #45792, .T. ) ;
#93752=CARTESIAN_POINT ( 'NONE',  ( 0.000000000000000000, 0.000000000000000000, 5.000000000000000000 ) ) ;
#93753=LINE ( 'NONE', #4523, #37967 ) ;
#93754=ORIENTED_EDGE ( 'NONE', *, *, #111046, .F. ) ;
#93755=CARTESIAN_POINT ( 'NONE',  ( 13.56687199751249473, -21.74070752338406365, 6.915939825044041811 ) ) ;
#93756=ORIENTED_EDGE ( 'NONE', *, *, #141158, .T. ) ;
#93759=EDGE_CURVE ( 'NONE', #83415, #54378, #134212, .T. ) ;
#93760=EDGE_CURVE ( 'NONE', #36959, #24621, #12406, .T. ) ;
#93761=DIRECTION ( 'NONE',  ( -0.3543493200069162685, -0.000000000000000000, -0.9351131265310288487 ) ) ;
#93762=VERTEX_POINT ( 'NONE', #10954 ) ;
#93763=DIRECTION ( 'NONE',  ( -0.000000000000000000, 0.000000000000000000, 1.000000000000000000 ) ) ;
#93764=DIRECTION ( 'NONE',  ( -0.7071067811865486830, -0.7071067811865464625, 0.000000000000000000 ) ) ;
#93765=CARTESIAN_POINT ( 'NONE',  ( 9.489213562373095101, -27.52281430457062328, 5.000000000000000000 ) ) ;
#93767=CARTESIAN_POINT ( 'NONE',  ( -34.92500000000001137, -8.671992264596164901, 16.70802535927751364 ) ) ;
#93769=LINE ( 'NONE', #16167, #104862 ) ;
#93771=EDGE_CURVE ( 'NONE', #92747, #20850, #34907, .T. ) ;
#93773=VERTEX_POINT ( 'NONE', #22545 ) ;
#93774=EDGE_CURVE ( 'NONE', #81952, #121450, #78398, .T. ) ;
#93775=EDGE_LOOP ( 'NONE', ( #90965, #8355, #121020, #47065 ) ) ;
#93776=LINE ( 'NONE', #6711, #91181 ) ;
#93779=CARTESIAN_POINT ( 'NONE',  ( 15.79289321881335084, 18.75929247661553489, 5.000000000000000000 ) ) ;
#93780=CARTESIAN_POINT ( 'NONE',  ( -34.49999999999975842, -5.945670655168998842, 4.994342998332166772 ) ) ;
#93781=DIRECTION ( 'NONE',  ( 0.3543493200069163240, 0.000000000000000000, 0.9351131265310288487 ) ) ;
#93782=ADVANCED_FACE ( 'NONE', ( #55953 ), #100155, .F. ) ;
#93783=DIRECTION ( 'NONE',  ( -0.6830127018922180770, -0.6830127018922204085, -0.2588190451025213501 ) ) ;
#93786=LINE ( 'NONE', #25664, #74701 ) ;
#93787=EDGE_CURVE ( 'NONE', #101003, #110282, #123348, .T. ) ;
#93790=CARTESIAN_POINT ( 'NONE',  ( -5.999999999999952927, -12.41253812416063340, 4.000000000000000000 ) ) ;
#93792=CARTESIAN_POINT ( 'NONE',  ( -26.99999999999981526, -5.527737879153217015, -7.983877177622316523 ) ) ;
#93793=ORIENTED_EDGE ( 'NONE', *, *, #63527, .T. ) ;
#93794=ORIENTED_EDGE ( 'NONE', *, *, #89638, .T. ) ;
#93796=CARTESIAN_POINT ( 'NONE',  ( 34.42499999999998295, -21.72500000000000142, 4.500000000000000888 ) ) ;
#93797=DIRECTION ( 'NONE',  ( 0.7071067811865487940, 0.7071067811865463515, -0.000000000000000000 ) ) ;
#93798=PLANE ( 'NONE',  #6897 ) ;
#93799=PLANE ( 'NONE',  #85813 ) ;
#93801=VERTEX_POINT ( 'NONE', #35638 ) ;
#93802=CARTESIAN_POINT ( 'NONE',  ( 30.79289321881324781, 3.759292476615681888, 5.000000000000000000 ) ) ;
#93803=DIRECTION ( 'NONE',  ( -0.7071067811865487940, 0.7071067811865463515, -0.000000000000000000 ) ) ;
#93805=ADVANCED_FACE ( 'NONE', ( #2214 ), #110278, .F. ) ;
#93806=CARTESIAN_POINT ( 'NONE',  ( -17.99999999999986500, 11.96639925780213609, 5.000000000000000000 ) ) ;
#93807=DIRECTION ( 'NONE',  ( 0.6830127018922181881, 0.6830127018922202975, -0.2588190451025214056 ) ) ;
#93812=VECTOR ( 'NONE', #129648, 999.9999999999998863 ) ;
#93814=EDGE_LOOP ( 'NONE', ( #3776, #18670, #102657, #8659 ) ) ;
#93817=CARTESIAN_POINT ( 'NONE',  ( 25.49999999999982592, -16.53360074219757081, 5.000000000000000000 ) ) ;
#93818=VECTOR ( 'NONE', #102029, 999.9999999999998863 ) ;
#93820=CARTESIAN_POINT ( 'NONE',  ( 13.08638746355377158, 2.894607053745207992, 4.324337194087679137 ) ) ;
#93821=ORIENTED_EDGE ( 'NONE', *, *, #47415, .F. ) ;
#93823=VECTOR ( 'NONE', #97894, 999.9999999999998863 ) ;
#93828=EDGE_LOOP ( 'NONE', ( #25727, #1772, #28777, #84738 ) ) ;
#93829=CARTESIAN_POINT ( 'NONE',  ( 34.42499999999998295, -21.72500000000000142, 0.4999999999999995559 ) ) ;
#93830=CARTESIAN_POINT ( 'NONE',  ( -8.207106781186485733, 15.75929247661555976, 5.000000000000000000 ) ) ;
#93832=LINE ( 'NONE', #72130, #141222 ) ;
#93833=LINE ( 'NONE', #126448, #48844 ) ;
#93834=CARTESIAN_POINT ( 'NONE',  ( -45.18398860626900415, 28.73617430169818832, 5.000000000000000000 ) ) ;
#93835=ORIENTED_EDGE ( 'NONE', *, *, #129314, .F. ) ;
#93836=LINE ( 'NONE', #125774, #4367 ) ;
#93837=PLANE ( 'NONE',  #36213 ) ;
#93838=DIRECTION ( 'NONE',  ( 0.6830127018922180770, -0.6830127018922204085, -0.2588190451025213501 ) ) ;
#93839=LINE ( 'NONE', #117698, #136446 ) ;
#93841=VERTEX_POINT ( 'NONE', #111740 ) ;
#93842=VECTOR ( 'NONE', #123558, 999.9999999999998863 ) ;
#93843=AXIS2_PLACEMENT_3D ( 'NONE', #13390, #135911, #69246 ) ;
#93844=ORIENTED_EDGE ( 'NONE', *, *, #2884, .T. ) ;
#93847=FACE_OUTER_BOUND ( 'NONE', #125026, .T. ) ;
#93848=EDGE_CURVE ( 'NONE', #76403, #63322, #124043, .T. ) ;
#93851=ORIENTED_EDGE ( 'NONE', *, *, #23184, .T. ) ;
#93852=ORIENTED_EDGE ( 'NONE', *, *, #35989, .T. ) ;
#93853=CARTESIAN_POINT ( 'NONE',  ( -57.18398860626899705, 28.73617430169827358, 5.000000000000000000 ) ) ;
#93854=ORIENTED_EDGE ( 'NONE', *, *, #136752, .F. ) ;
#93855=ORIENTED_EDGE ( 'NONE', *, *, #88009, .F. ) ;
#93856=PLANE ( 'NONE',  #5002 ) ;
#93857=ORIENTED_EDGE ( 'NONE', *, *, #4105, .F. ) ;
#93858=CARTESIAN_POINT ( 'NONE',  ( 0.000000000000000000, 0.000000000000000000, 5.000000000000000000 ) ) ;
#93859=CARTESIAN_POINT ( 'NONE',  ( 2.292893218813447209, 5.259292476615669010, 5.000000000000000000 ) ) ;
#93860=EDGE_CURVE ( 'NONE', #45084, #139004, #99396, .T. ) ;
#93861=FACE_BOUND ( 'NONE', #51009, .T. ) ;
#93864=EDGE_CURVE ( 'NONE', #95628, #136288, #13813, .T. ) ;
#93865=LINE ( 'NONE', #18988, #34427 ) ;
#93866=FACE_OUTER_BOUND ( 'NONE', #86128, .T. ) ;
#93868=EDGE_CURVE ( 'NONE', #59858, #18661, #68276, .T. ) ;
#93871=ORIENTED_EDGE ( 'NONE', *, *, #67597, .F. ) ;
#93872=ORIENTED_EDGE ( 'NONE', *, *, #35822, .F. ) ;
#93874=ORIENTED_EDGE ( 'NONE', *, *, #68231, .F. ) ;
#93876=CARTESIAN_POINT ( 'NONE',  ( 24.51665438641027350, 22.22500000000000142, 4.500000000000000888 ) ) ;
#93877=DIRECTION ( 'NONE',  ( 0.000000000000000000, -0.3543493200069153248, -0.9351131265310291818 ) ) ;
#93878=EDGE_CURVE ( 'NONE', #11057, #50067, #121167, .T. ) ;
#93879=LINE ( 'NONE', #39531, #58728 ) ;
#93880=ORIENTED_EDGE ( 'NONE', *, *, #78045, .T. ) ;
#93881=CARTESIAN_POINT ( 'NONE',  ( 33.70710678118631165, 17.25929247661554200, 5.000000000000000000 ) ) ;
#93882=DIRECTION ( 'NONE',  ( -0.7071067811865486830, -0.7071067811865464625, 0.000000000000000000 ) ) ;
#93883=CARTESIAN_POINT ( 'NONE',  ( -6.770042794577893375, 21.73644205237997085, 5.000000000000000888 ) ) ;
#93885=FACE_OUTER_BOUND ( 'NONE', #111696, .T. ) ;
#93886=PLANE ( 'NONE',  #16914 ) ;
#93888=EDGE_CURVE ( 'NONE', #5968, #44042, #114570, .T. ) ;
#93891=CARTESIAN_POINT ( 'NONE',  ( -32.99451991528749062, 28.92564299267960948, 4.000000000000000000 ) ) ;
#93892=CARTESIAN_POINT ( 'NONE',  ( 0.005480084712502889671, 28.92564299267938210, 4.000000000000000000 ) ) ;
#93893=VERTEX_POINT ( 'NONE', #15241 ) ;
#93894=VERTEX_POINT ( 'NONE', #25416 ) ;
#93895=ORIENTED_EDGE ( 'NONE', *, *, #118444, .F. ) ;
#93897=ADVANCED_FACE ( 'NONE', ( #103676 ), #125476, .F. ) ;
#93898=ORIENTED_EDGE ( 'NONE', *, *, #19255, .T. ) ;
#93902=VERTEX_POINT ( 'NONE', #26160 ) ;
#93903=AXIS2_PLACEMENT_3D ( 'NONE', #99000, #20008, #98320 ) ;
#93904=CARTESIAN_POINT ( 'NONE',  ( 0.000000000000000000, -0.8619312979532001151, -5.102805207349826233 ) ) ;
#93905=EDGE_CURVE ( 'NONE', #108114, #18661, #36325, .T. ) ;
#93906=EDGE_LOOP ( 'NONE', ( #99082, #126187, #37595, #111001 ) ) ;
#93907=CARTESIAN_POINT ( 'NONE',  ( 23.99999999999984013, 16.93112307739201583, 4.000000000000000000 ) ) ;
#93908=LINE ( 'NONE', #87335, #33646 ) ;
#93909=LINE ( 'NONE', #71461, #95676 ) ;
#93911=ORIENTED_EDGE ( 'NONE', *, *, #81805, .T. ) ;
#93912=DIRECTION ( 'NONE',  ( 0.7071067811865487940, -0.7071067811865463515, 0.000000000000000000 ) ) ;
#93913=FACE_OUTER_BOUND ( 'NONE', #12628, .T. ) ;
#93914=EDGE_CURVE ( 'NONE', #87047, #128314, #59520, .T. ) ;
#93915=ADVANCED_FACE ( 'NONE', ( #137057 ), #49367, .F. ) ;
#93917=CARTESIAN_POINT ( 'NONE',  ( -2.292893218813438772, -0.7407075233842805861, 5.000000000000000000 ) ) ;
#93918=ORIENTED_EDGE ( 'NONE', *, *, #85201, .T. ) ;
#93919=VECTOR ( 'NONE', #107699, 1000.000000000000000 ) ;
#93920=ORIENTED_EDGE ( 'NONE', *, *, #3122, .F. ) ;
#93921=ORIENTED_EDGE ( 'NONE', *, *, #38945, .T. ) ;
#93922=ORIENTED_EDGE ( 'NONE', *, *, #111827, .F. ) ;
#93923=DIRECTION ( 'NONE',  ( 0.6830127018922181881, 0.6830127018922202975, -0.2588190451025214056 ) ) ;
#93924=EDGE_CURVE ( 'NONE', #100628, #131755, #14560, .T. ) ;
#93925=CARTESIAN_POINT ( 'NONE',  ( -21.48921356237309155, -27.52281430457070499, 5.000000000000000000 ) ) ;
#93926=PLANE ( 'NONE',  #135071 ) ;
#93927=ADVANCED_FACE ( 'NONE', ( #93554 ), #37022, .F. ) ;
#93929=CARTESIAN_POINT ( 'NONE',  ( 0.4892135623730947680, -27.52281430457055578, 5.000000000000000000 ) ) ;
#93930=EDGE_LOOP ( 'NONE', ( #74569, #19245, #138739, #45499 ) ) ;
#93931=CARTESIAN_POINT ( 'NONE',  ( -27.48921356237309155, -27.52281430457074762, 5.000000000000000000 ) ) ;
#93932=AXIS2_PLACEMENT_3D ( 'NONE', #114333, #104139, #4803 ) ;
#93933=CARTESIAN_POINT ( 'NONE',  ( 0.000000000000000000, 0.000000000000000000, 5.000000000000000000 ) ) ;
#93934=LINE ( 'NONE', #117105, #117982 ) ;
#93936=CARTESIAN_POINT ( 'NONE',  ( -30.70710678118632231, 5.259292476615667233, 5.000000000000000000 ) ) ;
#93937=AXIS2_PLACEMENT_3D ( 'NONE', #125303, #91946, #45626 ) ;
#93940=ORIENTED_EDGE ( 'NONE', *, *, #81364, .T. ) ;
#93943=FACE_OUTER_BOUND ( 'NONE', #116260, .T. ) ;
#93946=CARTESIAN_POINT ( 'NONE',  ( -8.999999999999937828, 10.93112307739207267, 4.000000000000000000 ) ) ;
#93948=CARTESIAN_POINT ( 'NONE',  ( -34.42500000000001137, 22.22500000000000142, 0.4999999999999995559 ) ) ;
#93949=EDGE_CURVE ( 'NONE', #66852, #135458, #58841, .T. ) ;
#93952=PLANE ( 'NONE',  #52141 ) ;
#93954=CARTESIAN_POINT ( 'NONE',  ( -15.48921356237309510, -27.52281430457066236, 5.000000000000000000 ) ) ;
#93955=CARTESIAN_POINT ( 'NONE',  ( -69.18398860626899705, 28.73617430169835529, 5.000000000000000000 ) ) ;
#93956=DIRECTION ( 'NONE',  ( -0.000000000000000000, -0.3543493200069152693, 0.9351131265310292928 ) ) ;
#93957=CARTESIAN_POINT ( 'NONE',  ( -47.99451991528749062, 28.92564299267971251, 4.000000000000000000 ) ) ;
#93959=PLANE ( 'NONE',  #1313 ) ;
#93960=ORIENTED_EDGE ( 'NONE', *, *, #127452, .F. ) ;
#93962=CARTESIAN_POINT ( 'NONE',  ( -51.29974487139158867, -27.71228299555242103, 4.000000000000000000 ) ) ;
#93963=VERTEX_POINT ( 'NONE', #103003 ) ;
#93964=DIRECTION ( 'NONE',  ( -0.7071067811865486830, -0.7071067811865464625, 0.000000000000000000 ) ) ;
#93965=CARTESIAN_POINT ( 'NONE',  ( -18.52400138585436551, 22.03583458319438648, 4.979811245910084061 ) ) ;
#93966=VERTEX_POINT ( 'NONE', #38459 ) ;
#93968=CARTESIAN_POINT ( 'NONE',  ( -15.29974487139158867, -27.71228299555216879, 4.000000000000000000 ) ) ;
#93969=ORIENTED_EDGE ( 'NONE', *, *, #60393, .T. ) ;
#93970=PLANE ( 'NONE',  #972 ) ;
#93971=EDGE_CURVE ( 'NONE', #7076, #63600, #82684, .T. ) ;
#93973=DIRECTION ( 'NONE',  ( -0.000000000000000000, 0.3543493200069153248, 0.9351131265310292928 ) ) ;
#93975=VERTEX_POINT ( 'NONE', #136329 ) ;
#93976=ADVANCED_FACE ( 'NONE', ( #126866 ), #81269, .F. ) ;
#93977=DIRECTION ( 'NONE',  ( 0.7071067811865487940, -0.7071067811865463515, 0.000000000000000000 ) ) ;
#93978=DIRECTION ( 'NONE',  ( -0.7071067811865486830, 0.7071067811865464625, 0.000000000000000000 ) ) ;
#93982=ORIENTED_EDGE ( 'NONE', *, *, #14047, .F. ) ;
#93983=DIRECTION ( 'NONE',  ( 0.7071067811865486830, -0.7071067811865464625, -0.000000000000000000 ) ) ;
#93984=ORIENTED_EDGE ( 'NONE', *, *, #113419, .T. ) ;
#93986=DIRECTION ( 'NONE',  ( -0.000000000000000000, 0.000000000000000000, 1.000000000000000000 ) ) ;
#93987=PLANE ( 'NONE',  #14535 ) ;
#93988=CARTESIAN_POINT ( 'NONE',  ( 25.55334942336766346, 2.259292476615690770, 14.86850063742348560 ) ) ;
#93990=CARTESIAN_POINT ( 'NONE',  ( 11.48334561358946360, 22.22500000000000142, 4.500000000000000888 ) ) ;
#93993=DIRECTION ( 'NONE',  ( 0.6830127018922180770, -0.6830127018922204085, -0.2588190451025213501 ) ) ;
#93994=CARTESIAN_POINT ( 'NONE',  ( -29.48334561358934991, 22.22500000000000142, 4.500000000000000888 ) ) ;
#93995=VERTEX_POINT ( 'NONE', #94251 ) ;
#93996=CARTESIAN_POINT ( 'NONE',  ( 18.18398860626898994, 28.73617430169800002, 5.000000000000000000 ) ) ;
#93997=CARTESIAN_POINT ( 'NONE',  ( -34.92500000000001137, 13.70193056682087196, 4.500000000000000888 ) ) ;
#93999=DIRECTION ( 'NONE',  ( 0.7071067811865487940, -0.7071067811865463515, 0.000000000000000000 ) ) ;
#94000=ORIENTED_EDGE ( 'NONE', *, *, #102761, .F. ) ;
#94001=AXIS2_PLACEMENT_3D ( 'NONE', #126560, #91799, #82382 ) ;
#94002=ORIENTED_EDGE ( 'NONE', *, *, #97162, .F. ) ;
#94007=CARTESIAN_POINT ( 'NONE',  ( 0.1839886062690032631, 28.73617430169787568, 5.000000000000000000 ) ) ;
#94008=CARTESIAN_POINT ( 'NONE',  ( -30.48921356237309510, -27.52281430457076894, 5.000000000000000000 ) ) ;
#94009=DIRECTION ( 'NONE',  ( -0.000000000000000000, 0.3543493200069153248, 0.9351131265310292928 ) ) ;
#94010=ORIENTED_EDGE ( 'NONE', *, *, #132398, .F. ) ;
#94011=PLANE ( 'NONE',  #72383 ) ;
#94012=( BOUNDED_CURVE ( )  B_SPLINE_CURVE ( 3, ( #76408, #74255, #87979, #54655 ),
 .UNSPECIFIED., .F., .F. ) 
 B_SPLINE_CURVE_WITH_KNOTS ( ( 4, 4 ),
 ( 2.605825008650064500, 2.701628967222372779 ),
 .UNSPECIFIED. ) 
 CURVE ( )  GEOMETRIC_REPRESENTATION_ITEM ( )  RATIONAL_B_SPLINE_CURVE ( ( 1.000000000000000000, 0.9992352797041761381, 0.9992352797041761381, 1.000000000000000000 ) ) 
 REPRESENTATION_ITEM ( '' )  );
#94013=CARTESIAN_POINT ( 'NONE',  ( -33.32816939922331301, -21.74070752338406010, 4.000000000000000000 ) ) ;
#94014=EDGE_CURVE ( 'NONE', #6381, #136204, #135636, .T. ) ;
#94015=ORIENTED_EDGE ( 'NONE', *, *, #131889, .F. ) ;
#94016=VECTOR ( 'NONE', #129268, 1000.000000000000000 ) ;
#94017=DIRECTION ( 'NONE',  ( -0.7071067811865487940, 0.7071067811865463515, 0.000000000000000000 ) ) ;
#94019=LINE ( 'NONE', #72335, #70124 ) ;
#94021=ORIENTED_EDGE ( 'NONE', *, *, #64110, .F. ) ;
#94023=AXIS2_PLACEMENT_3D ( 'NONE', #40387, #104152, #39672 ) ;
#94024=PLANE ( 'NONE',  #116351 ) ;
#94025=EDGE_CURVE ( 'NONE', #14375, #26318, #89737, .T. ) ;
#94028=DIRECTION ( 'NONE',  ( -0.7071067811865487940, 0.7071067811865463515, 0.000000000000000000 ) ) ;
#94029=LINE ( 'NONE', #139723, #79050 ) ;
#94030=DIRECTION ( 'NONE',  ( 0.7071067811865487940, 0.7071067811865463515, -0.000000000000000000 ) ) ;
#94033=VECTOR ( 'NONE', #3097, 999.9999999999998863 ) ;
#94034=EDGE_CURVE ( 'NONE', #72846, #43398, #78167, .T. ) ;
#94035=ADVANCED_FACE ( 'NONE', ( #1963 ), #112222, .F. ) ;
#94036=CARTESIAN_POINT ( 'NONE',  ( -29.67183060077626067, -9.740707523384182664, 4.000000000000000000 ) ) ;
#94037=VERTEX_POINT ( 'NONE', #24479 ) ;
#94038=VECTOR ( 'NONE', #115168, 1000.000000000000000 ) ;
#94040=VERTEX_POINT ( 'NONE', #23779 ) ;
#94042=EDGE_CURVE ( 'NONE', #12475, #26153, #34679, .T. ) ;
#94043=VERTEX_POINT ( 'NONE', #1278 ) ;
#94044=AXIS2_PLACEMENT_3D ( 'NONE', #92718, #102909, #58741 ) ;
#94046=EDGE_CURVE ( 'NONE', #129574, #121582, #44865, .T. ) ;
#94048=VERTEX_POINT ( 'NONE', #124512 ) ;
#94049=CARTESIAN_POINT ( 'NONE',  ( 3.707106781186514599, 11.25929247661560062, 5.000000000000000000 ) ) ;
#94050=CARTESIAN_POINT ( 'NONE',  ( -34.92500000000001137, 21.72500000000000142, 5.000000000000000000 ) ) ;
#94051=DIRECTION ( 'NONE',  ( 0.6830127018922180770, -0.6830127018922204085, -0.2588190451025213501 ) ) ;
#94052=DIRECTION ( 'NONE',  ( -0.7071067811865486830, -0.7071067811865464625, 0.000000000000000000 ) ) ;
#94053=CARTESIAN_POINT ( 'NONE',  ( 33.29974487139158867, -27.71228299555229313, 4.000000000000000000 ) ) ;
#94054=ORIENTED_EDGE ( 'NONE', *, *, #10006, .T. ) ;
#94055=LINE ( 'NONE', #28822, #107365 ) ;
#94056=CARTESIAN_POINT ( 'NONE',  ( -34.92500000000001137, -22.22500000000000142, 4.000000000000000000 ) ) ;
#94057=EDGE_LOOP ( 'NONE', ( #64497, #712, #94521, #79233 ) ) ;
#94058=DIRECTION ( 'NONE',  ( 0.3543493200069164351, 2.781805975412904658E-17, -0.9351131265310288487 ) ) ;
#94059=ORIENTED_EDGE ( 'NONE', *, *, #64502, .F. ) ;
#94060=ORIENTED_EDGE ( 'NONE', *, *, #48127, .F. ) ;
#94061=DIRECTION ( 'NONE',  ( -0.7071067811865486830, 0.7071067811865464625, 0.000000000000000000 ) ) ;
#94062=ORIENTED_EDGE ( 'NONE', *, *, #132595, .F. ) ;
#94063=ORIENTED_EDGE ( 'NONE', *, *, #11403, .F. ) ;
#94066=ORIENTED_EDGE ( 'NONE', *, *, #133025, .T. ) ;
#94067=DIRECTION ( 'NONE',  ( -0.000000000000000000, 0.000000000000000000, 1.000000000000000000 ) ) ;
#94068=PLANE ( 'NONE',  #54351 ) ;
#94070=DIRECTION ( 'NONE',  ( -0.3543493200069162685, -0.000000000000000000, -0.9351131265310288487 ) ) ;
#94071=PLANE ( 'NONE',  #95312 ) ;
#94072=ADVANCED_FACE ( 'NONE', ( #22304 ), #46275, .F. ) ;
#94073=CARTESIAN_POINT ( 'NONE',  ( -21.48921356237309155, -27.52281430457070499, 5.000000000000000000 ) ) ;
#94074=LINE ( 'NONE', #29524, #73080 ) ;
#94076=CARTESIAN_POINT ( 'NONE',  ( 15.70710678118643955, -6.740707523384209310, 5.000000000000000000 ) ) ;
#94077=CARTESIAN_POINT ( 'NONE',  ( 34.47516574401890210, 4.490517612115580981, 4.998110765256833510 ) ) ;
#94078=EDGE_CURVE ( 'NONE', #3326, #118907, #89052, .T. ) ;
#94079=VERTEX_POINT ( 'NONE', #12873 ) ;
#94080=FACE_OUTER_BOUND ( 'NONE', #35098, .T. ) ;
#94081=ORIENTED_EDGE ( 'NONE', *, *, #27636, .T. ) ;
#94082=ADVANCED_FACE ( 'NONE', ( #57154 ), #67291, .F. ) ;
#94083=VERTEX_POINT ( 'NONE', #133959 ) ;
#94084=CARTESIAN_POINT ( 'NONE',  ( -17.99451991528748351, 28.92564299267950645, 4.000000000000000000 ) ) ;
#94085=VERTEX_POINT ( 'NONE', #55706 ) ;
#94086=EDGE_CURVE ( 'NONE', #100760, #36504, #101328, .T. ) ;
#94087=DIRECTION ( 'NONE',  ( 0.6830127018922181881, 0.6830127018922202975, -0.2588190451025214056 ) ) ;
#94089=LINE ( 'NONE', #115098, #30157 ) ;
#94091=ORIENTED_EDGE ( 'NONE', *, *, #47048, .T. ) ;
#94094=ADVANCED_FACE ( 'NONE', ( #80324 ), #111487, .F. ) ;
#94096=DIRECTION ( 'NONE',  ( 0.7071067811865487940, 0.7071067811865463515, 0.000000000000000000 ) ) ;
#94097=CARTESIAN_POINT ( 'NONE',  ( -2.999999999999975131, 7.007997736742443529, -8.085015511992120096 ) ) ;
#94098=EDGE_CURVE ( 'NONE', #20507, #2157, #11426, .T. ) ;
#94099=DIRECTION ( 'NONE',  ( 0.7071067811865487940, 0.7071067811865463515, 0.000000000000000000 ) ) ;
#94102=ORIENTED_EDGE ( 'NONE', *, *, #37365, .F. ) ;
#94103=DIRECTION ( 'NONE',  ( -0.7071067811865487940, 0.7071067811865463515, -0.000000000000000000 ) ) ;
#94104=DIRECTION ( 'NONE',  ( -0.000000000000000000, 0.000000000000000000, 1.000000000000000000 ) ) ;
#94105=CARTESIAN_POINT ( 'NONE',  ( -42.29974487139158157, -27.71228299555235708, 4.000000000000000000 ) ) ;
#94106=CARTESIAN_POINT ( 'NONE',  ( -54.29974487139159578, -27.71228299555243879, 4.000000000000000000 ) ) ;
#94107=LINE ( 'NONE', #14430, #60119 ) ;
#94108=CARTESIAN_POINT ( 'NONE',  ( 39.18398860626899705, 28.73617430169814568, 5.000000000000000000 ) ) ;
#94109=CARTESIAN_POINT ( 'NONE',  ( -57.18398860626899705, 28.73617430169827358, 5.000000000000000000 ) ) ;
#94110=EDGE_CURVE ( 'NONE', #72893, #120409, #36097, .T. ) ;
#94111=VECTOR ( 'NONE', #25044, 1000.000000000000000 ) ;
#94113=CARTESIAN_POINT ( 'NONE',  ( 10.49999999999993250, 8.319652575858395238, -8.582050562765804358 ) ) ;
#94114=VERTEX_POINT ( 'NONE', #99901 ) ;
#94115=DIRECTION ( 'NONE',  ( 0.7071067811865487940, 0.7071067811865463515, 0.000000000000000000 ) ) ;
#94116=FACE_OUTER_BOUND ( 'NONE', #99184, .T. ) ;
#94117=EDGE_LOOP ( 'NONE', ( #126819, #91470, #105744, #113222 ) ) ;
#94118=CARTESIAN_POINT ( 'NONE',  ( 9.328169399223460445, 5.259292476615662792, 4.000000000000000000 ) ) ;
#94120=ORIENTED_EDGE ( 'NONE', *, *, #1519, .T. ) ;
#94123=ORIENTED_EDGE ( 'NONE', *, *, #77626, .T. ) ;
#94124=DIRECTION ( 'NONE',  ( -0.7071067811865486830, 0.7071067811865463515, 0.000000000000000000 ) ) ;
#94126=ORIENTED_EDGE ( 'NONE', *, *, #102441, .F. ) ;
#94127=VECTOR ( 'NONE', #128796, 1000.000000000000000 ) ;
#94128=VECTOR ( 'NONE', #134168, 999.9999999999998863 ) ;
#94129=CARTESIAN_POINT ( 'NONE',  ( 13.49999999999991829, -17.94781430457064531, 5.000000000000000000 ) ) ;
#94130=PLANE ( 'NONE',  #11464 ) ;
#94132=VECTOR ( 'NONE', #82108, 1000.000000000000000 ) ;
#94135=DIRECTION ( 'NONE',  ( 0.7071067811865487940, -0.7071067811865463515, 0.000000000000000000 ) ) ;
#94136=LINE ( 'NONE', #125363, #495 ) ;
#94137=DIRECTION ( 'NONE',  ( -0.7071067811865487940, 0.7071067811865463515, -0.000000000000000000 ) ) ;
#94141=CARTESIAN_POINT ( 'NONE',  ( 22.49999999999984013, -12.08601207473287253, -10.46905243149099540 ) ) ;
#94142=VECTOR ( 'NONE', #12838, 999.9999999999998863 ) ;
#94143=CARTESIAN_POINT ( 'NONE',  ( -34.49999999999975842, 16.46425560840032176, 4.994342998332164107 ) ) ;
#94144=CARTESIAN_POINT ( 'NONE',  ( 34.45011844616451668, 15.00230414159378256, 5.000000000000000888 ) ) ;
#94145=ORIENTED_EDGE ( 'NONE', *, *, #109895, .F. ) ;
#94146=EDGE_CURVE ( 'NONE', #106377, #16785, #84005, .T. ) ;
#94147=EDGE_LOOP ( 'NONE', ( #16659, #104381, #30696, #119166, #1200, #29933 ) ) ;
#94149=EDGE_CURVE ( 'NONE', #27138, #49673, #122393, .T. ) ;
#94150=PLANE ( 'NONE',  #125384 ) ;
#94151=ORIENTED_EDGE ( 'NONE', *, *, #47539, .F. ) ;
#94152=EDGE_LOOP ( 'NONE', ( #5776, #116905, #50748, #40341 ) ) ;
#94153=LINE ( 'NONE', #81910, #57295 ) ;
#94154=LINE ( 'NONE', #26768, #92672 ) ;
#94155=CARTESIAN_POINT ( 'NONE',  ( -36.18398860626899705, 28.73617430169812437, 5.000000000000000000 ) ) ;
#94157=CARTESIAN_POINT ( 'NONE',  ( -27.18398860626900060, 28.73617430169806042, 5.000000000000000000 ) ) ;
#94158=DIRECTION ( 'NONE',  ( 0.7071067811865487940, 0.7071067811865463515, 0.000000000000000000 ) ) ;
#94159=DIRECTION ( 'NONE',  ( -0.7071067811865487940, 0.7071067811865463515, 0.000000000000000000 ) ) ;
#94160=CARTESIAN_POINT ( 'NONE',  ( 7.499999999999954703, 10.08746187583913922, 4.000000000000000000 ) ) ;
#94161=EDGE_CURVE ( 'NONE', #34897, #87113, #4925, .T. ) ;
#94162=PLANE ( 'NONE',  #56348 ) ;
#94164=FACE_OUTER_BOUND ( 'NONE', #21731, .T. ) ;
#94165=LINE ( 'NONE', #71030, #38279 ) ;
#94166=LINE ( 'NONE', #72480, #33179 ) ;
#94167=CARTESIAN_POINT ( 'NONE',  ( -42.18398860626899705, 28.73617430169816700, 5.000000000000000000 ) ) ;
#94168=DIRECTION ( 'NONE',  ( -0.6830127018922181881, 0.6830127018922202975, -0.2588190451025214056 ) ) ;
#94170=ORIENTED_EDGE ( 'NONE', *, *, #42970, .T. ) ;
#94171=ORIENTED_EDGE ( 'NONE', *, *, #10257, .F. ) ;
#94174=( BOUNDED_CURVE ( )  B_SPLINE_CURVE ( 3, ( #87353, #86652, #130153, #19929 ),
 .UNSPECIFIED., .F., .T. ) 
 B_SPLINE_CURVE_WITH_KNOTS ( ( 4, 4 ),
 ( 5.920967161967927161, 7.341195215986648037 ),
 .UNSPECIFIED. ) 
 CURVE ( )  GEOMETRIC_REPRESENTATION_ITEM ( )  RATIONAL_B_SPLINE_CURVE ( ( 1.000000000000000000, 0.8388583629366591632, 0.8388583629366591632, 1.000000000000000000 ) ) 
 REPRESENTATION_ITEM ( '' )  );
#94175=ORIENTED_EDGE ( 'NONE', *, *, #19281, .F. ) ;
#94177=VECTOR ( 'NONE', #75482, 1000.000000000000000 ) ;
#94179=ORIENTED_EDGE ( 'NONE', *, *, #17686, .F. ) ;
#94183=VERTEX_POINT ( 'NONE', #60090 ) ;
#94184=CARTESIAN_POINT ( 'NONE',  ( 9.183988606268997046, 28.73617430169793607, 5.000000000000000000 ) ) ;
#94185=VERTEX_POINT ( 'NONE', #137653 ) ;
#94186=LINE ( 'NONE', #26805, #59288 ) ;
#94187=VECTOR ( 'NONE', #58196, 1000.000000000000000 ) ;
#94188=LINE ( 'NONE', #140552, #24031 ) ;
#94189=PLANE ( 'NONE',  #38482 ) ;
#94190=CARTESIAN_POINT ( 'NONE',  ( -29.99999999999979039, -21.41253812416053393, 4.000000000000000000 ) ) ;
#94191=ADVANCED_FACE ( 'NONE', ( #17955 ), #126731, .F. ) ;
#94192=ORIENTED_EDGE ( 'NONE', *, *, #35233, .F. ) ;
#94193=ORIENTED_EDGE ( 'NONE', *, *, #9618, .T. ) ;
#94194=VECTOR ( 'NONE', #10066, 1000.000000000000227 ) ;
#94196=CARTESIAN_POINT ( 'NONE',  ( -2.700255128608413990, -27.71228299555204089, 4.000000000000000000 ) ) ;
#94197=EDGE_CURVE ( 'NONE', #55296, #47325, #60835, .T. ) ;
#94198=DIRECTION ( 'NONE',  ( -0.000000000000000000, -0.3543493200069152693, 0.9351131265310292928 ) ) ;
#94200=CARTESIAN_POINT ( 'NONE',  ( 13.49999999999990052, -6.839392718269117211, -8.480912228396118024 ) ) ;
#94201=VECTOR ( 'NONE', #37198, 999.9999999999998863 ) ;
#94202=EDGE_CURVE ( 'NONE', #79985, #125649, #104993, .T. ) ;
#94204=CARTESIAN_POINT ( 'NONE',  ( -5.292893218813416567, -3.740707523384244837, 5.000000000000000000 ) ) ;
#94206=ORIENTED_EDGE ( 'NONE', *, *, #131568, .T. ) ;
#94207=VECTOR ( 'NONE', #66254, 1000.000000000000000 ) ;
#94209=CARTESIAN_POINT ( 'NONE',  ( 8.671830600776420539, 2.259292476615701428, 4.000000000000000000 ) ) ;
#94210=ADVANCED_FACE ( 'NONE', ( #82543 ), #71674, .F. ) ;
#94211=ORIENTED_EDGE ( 'NONE', *, *, #30221, .F. ) ;
#94212=EDGE_LOOP ( 'NONE', ( #126236, #13746, #128535, #65757 ) ) ;
#94213=EDGE_CURVE ( 'NONE', #106218, #18107, #117278, .T. ) ;
#94215=EDGE_CURVE ( 'NONE', #127624, #112797, #28163, .T. ) ;
#94216=DIRECTION ( 'NONE',  ( -0.7071067811865486830, 0.7071067811865464625, 0.000000000000000000 ) ) ;
#94217=DIRECTION ( 'NONE',  ( -0.000000000000000000, 0.3543493200069153248, 0.9351131265310292928 ) ) ;
#94218=ORIENTED_EDGE ( 'NONE', *, *, #104414, .T. ) ;
#94223=VERTEX_POINT ( 'NONE', #48478 ) ;
#94224=EDGE_CURVE ( 'NONE', #105583, #19893, #29568, .T. ) ;
#94225=DIRECTION ( 'NONE',  ( 0.7071067811865487940, 0.7071067811865463515, 0.000000000000000000 ) ) ;
#94226=VECTOR ( 'NONE', #24497, 1000.000000000000000 ) ;
#94227=FACE_BOUND ( 'NONE', #15574, .T. ) ;
#94228=ORIENTED_EDGE ( 'NONE', *, *, #120213, .F. ) ;
#94230=LINE ( 'NONE', #71800, #129116 ) ;
#94231=DIRECTION ( 'NONE',  ( 0.6830127018922181881, 0.6830127018922202975, -0.2588190451025214056 ) ) ;
#94232=ORIENTED_EDGE ( 'NONE', *, *, #54184, .T. ) ;
#94233=DIRECTION ( 'NONE',  ( 0.7071067811865487940, 0.7071067811865463515, 0.000000000000000000 ) ) ;
#94234=ORIENTED_EDGE ( 'NONE', *, *, #6424, .F. ) ;
#94235=ORIENTED_EDGE ( 'NONE', *, *, #101511, .F. ) ;
#94236=ADVANCED_FACE ( 'NONE', ( #95545 ), #61539, .T. ) ;
#94238=EDGE_LOOP ( 'NONE', ( #26676, #10145, #85650, #129049 ) ) ;
#94240=CIRCLE ( 'NONE', #91965, 5.968999999999998529 ) ;
#94242=VERTEX_POINT ( 'NONE', #73806 ) ;
#94243=DIRECTION ( 'NONE',  ( -0.000000000000000000, 0.3543493200069153248, 0.9351131265310292928 ) ) ;
#94245=DIRECTION ( 'NONE',  ( -0.000000000000000000, 0.3543493200069153248, 0.9351131265310292928 ) ) ;
#94247=DIRECTION ( 'NONE',  ( 0.6830127018922180770, -0.6830127018922204085, -0.2588190451025213501 ) ) ;
#94249=DIRECTION ( 'NONE',  ( 0.6830127018922180770, -0.6830127018922204085, -0.2588190451025213501 ) ) ;
#94251=CARTESIAN_POINT ( 'NONE',  ( 26.29387692260786480, 22.22500000000000142, 4.000000000000000000 ) ) ;
#94252=PLANE ( 'NONE',  #59899 ) ;
#94253=DIRECTION ( 'NONE',  ( 0.7071067811865487940, 0.7071067811865463515, 0.000000000000000000 ) ) ;
#94254=ORIENTED_EDGE ( 'NONE', *, *, #7157, .T. ) ;
#94255=EDGE_CURVE ( 'NONE', #59374, #34536, #105685, .T. ) ;
#94256=VERTEX_POINT ( 'NONE', #6348 ) ;
#94257=EDGE_LOOP ( 'NONE', ( #37711, #36796, #37743, #16419 ) ) ;
#94258=ORIENTED_EDGE ( 'NONE', *, *, #86785, .F. ) ;
#94260=VERTEX_POINT ( 'NONE', #50626 ) ;
#94261=EDGE_CURVE ( 'NONE', #111218, #91520, #94808, .T. ) ;
#94262=ORIENTED_EDGE ( 'NONE', *, *, #86468, .F. ) ;
#94264=CARTESIAN_POINT ( 'NONE',  ( 0.7928932188134510950, -8.240707523384198652, 5.000000000000000000 ) ) ;
#94265=DIRECTION ( 'NONE',  ( -0.7071067811865486830, -0.7071067811865464625, 0.000000000000000000 ) ) ;
#94266=EDGE_LOOP ( 'NONE', ( #6153, #18936, #94683, #85849 ) ) ;
#94267=VECTOR ( 'NONE', #50775, 1000.000000000000000 ) ;
#94268=LINE ( 'NONE', #138505, #69599 ) ;
#94269=EDGE_LOOP ( 'NONE', ( #38614, #40744, #12946, #24423 ) ) ;
#94270=ADVANCED_FACE ( 'NONE', ( #120859 ), #120120, .F. ) ;
#94271=LINE ( 'NONE', #29027, #120791 ) ;
#94272=CARTESIAN_POINT ( 'NONE',  ( 5.999999999999963585, 4.384688058510572972, -7.090945410444669861 ) ) ;
#94273=VECTOR ( 'NONE', #133796, 1000.000000000000000 ) ;
#94275=ORIENTED_EDGE ( 'NONE', *, *, #79518, .T. ) ;
#94277=CARTESIAN_POINT ( 'NONE',  ( 17.81601139373099940, 28.73617430169775133, 5.000000000000000000 ) ) ;
#94278=DIRECTION ( 'NONE',  ( 0.3543493200069162685, -0.000000000000000000, -0.9351131265310288487 ) ) ;
#94280=EDGE_LOOP ( 'NONE', ( #623, #65756, #64390, #31393 ) ) ;
#94281=ORIENTED_EDGE ( 'NONE', *, *, #71274, .T. ) ;
#94283=VERTEX_POINT ( 'NONE', #96937 ) ;
#94286=DIRECTION ( 'NONE',  ( -0.000000000000000000, 0.000000000000000000, 1.000000000000000000 ) ) ;
#94287=DIRECTION ( 'NONE',  ( -0.7071067811865486830, -0.7071067811865464625, 0.000000000000000000 ) ) ;
#94288=CARTESIAN_POINT ( 'NONE',  ( 3.792893218813431222, 0.7592924766157120864, 5.000000000000000000 ) ) ;
#94289=VERTEX_POINT ( 'NONE', #44038 ) ;
#94290=DIRECTION ( 'NONE',  ( -0.6830127018922181881, 0.6830127018922202975, -0.2588190451025214056 ) ) ;
#94292=CARTESIAN_POINT ( 'NONE',  ( 0.000000000000000000, -8.151047557385066256, -8.977947279169798733 ) ) ;
#94293=VECTOR ( 'NONE', #4969, 999.9999999999998863 ) ;
#94294=EDGE_LOOP ( 'NONE', ( #61666, #91100, #82289, #119423 ) ) ;
#94295=LINE ( 'NONE', #93600, #127620 ) ;
#94296=CARTESIAN_POINT ( 'NONE',  ( -63.18398860626900415, 28.73617430169831621, 5.000000000000000000 ) ) ;
#94297=EDGE_LOOP ( 'NONE', ( #1528, #95073, #31941, #25970 ) ) ;
#94299=ORIENTED_EDGE ( 'NONE', *, *, #51693, .T. ) ;
#94300=EDGE_CURVE ( 'NONE', #59468, #114684, #62956, .T. ) ;
#94301=ADVANCED_FACE ( 'NONE', ( #107133 ), #65092, .F. ) ;
#94302=EDGE_LOOP ( 'NONE', ( #7252, #11973, #122927, #14508 ) ) ;
#94303=CARTESIAN_POINT ( 'NONE',  ( 7.499999999999951150, 3.431123077392156162, 4.000000000000000000 ) ) ;
#94304=CARTESIAN_POINT ( 'NONE',  ( -34.75611968250421313, -19.29434930147574079, 4.955485411084900704 ) ) ;
#94305=ORIENTED_EDGE ( 'NONE', *, *, #56130, .F. ) ;
#94306=DIRECTION ( 'NONE',  ( -0.7071067811865486830, 0.7071067811865464625, 0.000000000000000000 ) ) ;
#94308=DIRECTION ( 'NONE',  ( -0.7071067811865487940, 0.7071067811865463515, 0.000000000000000000 ) ) ;
#94309=EDGE_CURVE ( 'NONE', #142977, #63081, #76687, .T. ) ;
#94310=DIRECTION ( 'NONE',  ( -0.000000000000000000, -0.3543493200069152693, 0.9351131265310292928 ) ) ;
#94313=EDGE_LOOP ( 'NONE', ( #44242, #134402, #130164, #122695 ) ) ;
#94314=PLANE ( 'NONE',  #67063 ) ;
#94315=LINE ( 'NONE', #81335, #44313 ) ;
#94316=LINE ( 'NONE', #50120, #108990 ) ;
#94317=CARTESIAN_POINT ( 'NONE',  ( 18.43680103220818367, -12.74070752338415247, 9.898150129686332122 ) ) ;
#94318=CARTESIAN_POINT ( 'NONE',  ( 6.183988606268994381, 28.73617430169791476, 5.000000000000000000 ) ) ;
#94319=DIRECTION ( 'NONE',  ( -0.000000000000000000, 0.000000000000000000, 1.000000000000000000 ) ) ;
#94321=LINE ( 'NONE', #40677, #148 ) ;
#94322=EDGE_CURVE ( 'NONE', #69532, #112039, #108527, .T. ) ;
#94323=CARTESIAN_POINT ( 'NONE',  ( -53.99451991528749062, 28.92564299267975869, 4.000000000000000000 ) ) ;
#94324=ORIENTED_EDGE ( 'NONE', *, *, #82528, .T. ) ;
#94325=ORIENTED_EDGE ( 'NONE', *, *, #117163, .F. ) ;
#94326=VERTEX_POINT ( 'NONE', #132509 ) ;
#94328=ADVANCED_FACE ( 'NONE', ( #129591 ), #31728, .F. ) ;
#94329=ORIENTED_EDGE ( 'NONE', *, *, #36306, .T. ) ;
#94331=ORIENTED_EDGE ( 'NONE', *, *, #80962, .F. ) ;
#94334=VERTEX_POINT ( 'NONE', #87536 ) ;
#94335=AXIS2_PLACEMENT_3D ( 'NONE', #89801, #12941, #91270 ) ;
#94336=CARTESIAN_POINT ( 'NONE',  ( -5.994519915287488843, 28.92564299267942118, 4.000000000000000000 ) ) ;
#94340=DIRECTION ( 'NONE',  ( -0.000000000000000000, -0.3543493200069152693, 0.9351131265310292928 ) ) ;
#94342=ORIENTED_EDGE ( 'NONE', *, *, #26515, .T. ) ;
#94343=ADVANCED_FACE ( 'NONE', ( #75257 ), #20111, .F. ) ;
#94344=CARTESIAN_POINT ( 'NONE',  ( -30.52400138585428380, 22.03583458319438293, 4.979811245910084949 ) ) ;
#94346=DIRECTION ( 'NONE',  ( 0.3543493200069162685, -0.000000000000000000, -0.9351131265310288487 ) ) ;
#94348=AXIS2_PLACEMENT_3D ( 'NONE', #86940, #120976, #74653 ) ;
#94349=PLANE ( 'NONE',  #116337 ) ;
#94351=CARTESIAN_POINT ( 'NONE',  ( 18.29974487139159223, -27.71228299555219010, 4.000000000000000000 ) ) ;
#94352=CARTESIAN_POINT ( 'NONE',  ( 62.99451991528749772, 28.92564299267982264, 4.000000000000000000 ) ) ;
#94353=ORIENTED_EDGE ( 'NONE', *, *, #138799, .F. ) ;
#94354=VERTEX_POINT ( 'NONE', #99090 ) ;
#94357=DIRECTION ( 'NONE',  ( 0.6830127018922181881, 0.6830127018922202975, -0.2588190451025214056 ) ) ;
#94358=FACE_OUTER_BOUND ( 'NONE', #33948, .T. ) ;
#94359=AXIS2_PLACEMENT_3D ( 'NONE', #122179, #46840, #91026 ) ;
#94360=DIRECTION ( 'NONE',  ( 1.000000000000000000, 0.000000000000000000, 0.000000000000000000 ) ) ;
#94362=LINE ( 'NONE', #63901, #14003 ) ;
#94364=VERTEX_POINT ( 'NONE', #41900 ) ;
#94365=CARTESIAN_POINT ( 'NONE',  ( -14.51078643762690490, -27.52281430457045275, 5.000000000000000000 ) ) ;
#94366=ORIENTED_EDGE ( 'NONE', *, *, #17501, .F. ) ;
#94367=DIRECTION ( 'NONE',  ( -0.6830127018922180770, -0.6830127018922204085, -0.2588190451025213501 ) ) ;
#94368=FACE_OUTER_BOUND ( 'NONE', #10939, .T. ) ;
#94369=LINE ( 'NONE', #81402, #129733 ) ;
#94370=ORIENTED_EDGE ( 'NONE', *, *, #139829, .F. ) ;
#94372=VERTEX_POINT ( 'NONE', #9961 ) ;
#94373=DIRECTION ( 'NONE',  ( -0.000000000000000000, 0.000000000000000000, 1.000000000000000000 ) ) ;
#94376=VECTOR ( 'NONE', #110618, 1000.000000000000000 ) ;
#94377=DIRECTION ( 'NONE',  ( 0.7071067811865487940, 0.7071067811865463515, -0.000000000000000000 ) ) ;
#94378=EDGE_CURVE ( 'NONE', #69087, #39740, #33195, .T. ) ;
#94380=EDGE_CURVE ( 'NONE', #108173, #138852, #53485, .T. ) ;
#94381=ORIENTED_EDGE ( 'NONE', *, *, #93860, .T. ) ;
#94382=EDGE_CURVE ( 'NONE', #68681, #16426, #140927, .T. ) ;
#94383=DIRECTION ( 'NONE',  ( -0.000000000000000000, 0.000000000000000000, 1.000000000000000000 ) ) ;
#94388=CARTESIAN_POINT ( 'NONE',  ( 5.292893218813416567, 11.25929247661560595, 5.000000000000000000 ) ) ;
#94389=ORIENTED_EDGE ( 'NONE', *, *, #48962, .T. ) ;
#94390=EDGE_CURVE ( 'NONE', #5826, #66103, #80840, .T. ) ;
#94392=PLANE ( 'NONE',  #141770 ) ;
#94393=ORIENTED_EDGE ( 'NONE', *, *, #96121, .T. ) ;
#94395=CARTESIAN_POINT ( 'NONE',  ( 20.99999999999985079, -3.033600742197708477, 5.000000000000000000 ) ) ;
#94397=FACE_BOUND ( 'NONE', #36231, .T. ) ;
#94398=EDGE_CURVE ( 'NONE', #121582, #105496, #45492, .T. ) ;
#94399=CARTESIAN_POINT ( 'NONE',  ( 0.000000000000000000, 14.87792677143809073, -11.06722581663439975 ) ) ;
#94400=DIRECTION ( 'NONE',  ( -0.3543493200069162685, -0.000000000000000000, -0.9351131265310288487 ) ) ;
#94401=DIRECTION ( 'NONE',  ( 0.7071067811865487940, -0.7071067811865463515, 0.000000000000000000 ) ) ;
#94402=EDGE_LOOP ( 'NONE', ( #116583, #33852, #64835 ) ) ;
#94403=CARTESIAN_POINT ( 'NONE',  ( 0.000000000000000000, 0.000000000000000000, 5.000000000000000000 ) ) ;
#94404=DIRECTION ( 'NONE',  ( 0.7071067811865486830, -0.7071067811865464625, -0.000000000000000000 ) ) ;
#94405=ORIENTED_EDGE ( 'NONE', *, *, #108426, .T. ) ;
#94406=VERTEX_POINT ( 'NONE', #113551 ) ;
#94407=CARTESIAN_POINT ( 'NONE',  ( -2.999999999999976463, -9.033600742197648970, 5.000000000000000000 ) ) ;
#94409=ORIENTED_EDGE ( 'NONE', *, *, #27077, .T. ) ;
#94410=VERTEX_POINT ( 'NONE', #89669 ) ;
#94412=ORIENTED_EDGE ( 'NONE', *, *, #142945, .F. ) ;
#94413=VECTOR ( 'NONE', #21333, 1000.000000000000000 ) ;
#94415=DIRECTION ( 'NONE',  ( -0.7071067811865486830, -0.7071067811865464625, -0.000000000000000000 ) ) ;
#94416=ORIENTED_EDGE ( 'NONE', *, *, #21947, .T. ) ;
#94418=AXIS2_PLACEMENT_3D ( 'NONE', #90809, #45883, #37860 ) ;
#94419=DIRECTION ( 'NONE',  ( -0.6830127018922180770, -0.6830127018922204085, -0.2588190451025213501 ) ) ;
#94421=CARTESIAN_POINT ( 'NONE',  ( 27.70710678118635073, 17.25929247661554200, 5.000000000000000000 ) ) ;
#94422=DIRECTION ( 'NONE',  ( -0.000000000000000000, 0.000000000000000000, 1.000000000000000000 ) ) ;
#94423=CARTESIAN_POINT ( 'NONE',  ( 26.81601139373100651, 28.73617430169768738, 5.000000000000000000 ) ) ;
#94424=ORIENTED_EDGE ( 'NONE', *, *, #102796, .F. ) ;
#94425=EDGE_CURVE ( 'NONE', #55296, #108338, #124441, .T. ) ;
#94426=ORIENTED_EDGE ( 'NONE', *, *, #81693, .F. ) ;
#94427=CARTESIAN_POINT ( 'NONE',  ( -45.48921356237309510, -27.52281430457087197, 5.000000000000000000 ) ) ;
#94428=AXIS2_PLACEMENT_3D ( 'NONE', #289, #1014, #22058 ) ;
#94430=VERTEX_POINT ( 'NONE', #134633 ) ;
#94431=ORIENTED_EDGE ( 'NONE', *, *, #33814, .T. ) ;
#94432=VECTOR ( 'NONE', #46694, 1000.000000000000000 ) ;
#94433=VERTEX_POINT ( 'NONE', #136028 ) ;
#94434=DIRECTION ( 'NONE',  ( -0.7071067811865486830, -0.7071067811865464625, 0.000000000000000000 ) ) ;
#94435=CARTESIAN_POINT ( 'NONE',  ( 15.29974487139158867, -27.71228299555216879, 4.000000000000000000 ) ) ;
#94436=ORIENTED_EDGE ( 'NONE', *, *, #40631, .F. ) ;
#94437=DIRECTION ( 'NONE',  ( -0.7071067811865486830, -0.7071067811865464625, 0.000000000000000000 ) ) ;
#94438=VECTOR ( 'NONE', #84984, 1000.000000000000000 ) ;
#94439=VECTOR ( 'NONE', #71258, 999.9999999999998863 ) ;
#94440=EDGE_CURVE ( 'NONE', #97859, #121120, #67846, .T. ) ;
#94441=DIRECTION ( 'NONE',  ( -1.000000000000000000, 0.000000000000000000, -0.000000000000000000 ) ) ;
#94443=FACE_OUTER_BOUND ( 'NONE', #103750, .T. ) ;
#94444=ORIENTED_EDGE ( 'NONE', *, *, #49627, .F. ) ;
#94445=LINE ( 'NONE', #80921, #126144 ) ;
#94446=CARTESIAN_POINT ( 'NONE',  ( -8.510786437626906675, -27.52281430457049183, 5.000000000000000000 ) ) ;
#94447=ADVANCED_FACE ( 'NONE', ( #123755 ), #11355, .F. ) ;
#94449=FACE_OUTER_BOUND ( 'NONE', #46107, .T. ) ;
#94450=ORIENTED_EDGE ( 'NONE', *, *, #108097, .F. ) ;
#94451=CARTESIAN_POINT ( 'NONE',  ( 9.489213562373095101, -27.52281430457062328, 5.000000000000000000 ) ) ;
#94452=ORIENTED_EDGE ( 'NONE', *, *, #12227, .F. ) ;
#94453=PLANE ( 'NONE',  #102863 ) ;
#94454=LINE ( 'NONE', #93041, #39913 ) ;
#94455=DIRECTION ( 'NONE',  ( -0.7071067811865486830, 0.7071067811865464625, 0.000000000000000000 ) ) ;
#94456=ORIENTED_EDGE ( 'NONE', *, *, #54646, .F. ) ;
#94457=EDGE_CURVE ( 'NONE', #96671, #99871, #35328, .T. ) ;
#94458=FACE_OUTER_BOUND ( 'NONE', #8209, .T. ) ;
#94459=CARTESIAN_POINT ( 'NONE',  ( 11.51078643762690490, -27.52281430457047406, 5.000000000000000000 ) ) ;
#94460=DIRECTION ( 'NONE',  ( -0.7071067811865486830, -0.7071067811865464625, 0.000000000000000000 ) ) ;
#94462=DIRECTION ( 'NONE',  ( -0.6830127018922181881, 0.6830127018922202975, -0.2588190451025214056 ) ) ;
#94463=LINE ( 'NONE', #27791, #134950 ) ;
#94465=AXIS2_PLACEMENT_3D ( 'NONE', #6714, #50998, #82919 ) ;
#94466=FACE_OUTER_BOUND ( 'NONE', #68670, .T. ) ;
#94467=LINE ( 'NONE', #114777, #34584 ) ;
#94468=ORIENTED_EDGE ( 'NONE', *, *, #29548, .F. ) ;
#94469=EDGE_CURVE ( 'NONE', #134257, #49377, #121573, .T. ) ;
#94470=ORIENTED_EDGE ( 'NONE', *, *, #44479, .F. ) ;
#94471=VECTOR ( 'NONE', #34180, 999.9999999999998863 ) ;
#94472=PLANE ( 'NONE',  #102753 ) ;
#94475=CARTESIAN_POINT ( 'NONE',  ( -8.816011393731004731, 28.73617430169781173, 5.000000000000000000 ) ) ;
#94476=CARTESIAN_POINT ( 'NONE',  ( 10.49999999999992717, -10.91253812416064584, 4.000000000000000000 ) ) ;
#94477=LINE ( 'NONE', #6012, #122370 ) ;
#94478=FACE_OUTER_BOUND ( 'NONE', #42918, .T. ) ;
#94479=ORIENTED_EDGE ( 'NONE', *, *, #136249, .T. ) ;
#94480=DIRECTION ( 'NONE',  ( 0.7071067811865486830, -0.7071067811865464625, -0.000000000000000000 ) ) ;
#94481=DIRECTION ( 'NONE',  ( 0.7071067811865487940, 0.7071067811865463515, -0.000000000000000000 ) ) ;
#94483=VECTOR ( 'NONE', #116723, 1000.000000000000000 ) ;
#94484=CARTESIAN_POINT ( 'NONE',  ( 18.18398860626898994, 28.73617430169800002, 5.000000000000000000 ) ) ;
#94486=FACE_OUTER_BOUND ( 'NONE', #111648, .T. ) ;
#94488=VERTEX_POINT ( 'NONE', #58537 ) ;
#94489=EDGE_CURVE ( 'NONE', #110945, #116780, #88981, .T. ) ;
#94490=VERTEX_POINT ( 'NONE', #133207 ) ;
#94492=CARTESIAN_POINT ( 'NONE',  ( 30.70710678118633652, -3.740707523384241728, 5.000000000000000000 ) ) ;
#94493=CARTESIAN_POINT ( 'NONE',  ( -8.292893218813395251, -9.740707523384186217, 5.000000000000000000 ) ) ;
#94494=CARTESIAN_POINT ( 'NONE',  ( -15.48921356237309510, -27.52281430457066236, 5.000000000000000000 ) ) ;
#94495=CARTESIAN_POINT ( 'NONE',  ( 29.99451991528749417, 28.92564299267958816, 4.000000000000000000 ) ) ;
#94496=EDGE_CURVE ( 'NONE', #107904, #37138, #12809, .T. ) ;
#94499=ORIENTED_EDGE ( 'NONE', *, *, #32440, .F. ) ;
#94500=ADVANCED_FACE ( 'NONE', ( #102705 ), #24415, .F. ) ;
#94501=DIRECTION ( 'NONE',  ( -0.7071067811865486830, -0.7071067811865464625, -0.000000000000000000 ) ) ;
#94502=CARTESIAN_POINT ( 'NONE',  ( 5.671830600776430309, 14.25929247661557397, 4.000000000000000000 ) ) ;
#94503=DIRECTION ( 'NONE',  ( -0.7071067811865486830, -0.7071067811865464625, 0.000000000000000000 ) ) ;
#94504=PLANE ( 'NONE',  #21888 ) ;
#94505=LINE ( 'NONE', #72103, #68910 ) ;
#94507=DIRECTION ( 'NONE',  ( 1.000000000000000000, 0.000000000000000000, 0.000000000000000000 ) ) ;
#94508=ORIENTED_EDGE ( 'NONE', *, *, #36440, .F. ) ;
#94510=AXIS2_PLACEMENT_3D ( 'NONE', #62538, #89270, #66805 ) ;
#94512=DIRECTION ( 'NONE',  ( -0.6830127018922180770, -0.6830127018922204085, -0.2588190451025213501 ) ) ;
#94513=FACE_OUTER_BOUND ( 'NONE', #82114, .T. ) ;
#94514=VERTEX_POINT ( 'NONE', #135349 ) ;
#94516=FACE_OUTER_BOUND ( 'NONE', #97805, .T. ) ;
#94517=AXIS2_PLACEMENT_3D ( 'NONE', #122636, #134986, #79186 ) ;
#94518=DIRECTION ( 'NONE',  ( 0.7071067811865486830, -0.7071067811865464625, -0.000000000000000000 ) ) ;
#94520=CARTESIAN_POINT ( 'NONE',  ( 0.4598383894973967490, 18.75929247661552779, 8.305906642995486422 ) ) ;
#94521=ORIENTED_EDGE ( 'NONE', *, *, #93291, .T. ) ;
#94522=ORIENTED_EDGE ( 'NONE', *, *, #123216, .F. ) ;
#94526=CARTESIAN_POINT ( 'NONE',  ( 2.510786437626908008, -27.52281430457053446, 5.000000000000000000 ) ) ;
#94527=DIRECTION ( 'NONE',  ( -0.000000000000000000, 0.000000000000000000, 1.000000000000000000 ) ) ;
#94528=VECTOR ( 'NONE', #114873, 999.9999999999998863 ) ;
#94529=CARTESIAN_POINT ( 'NONE',  ( -8.999999999999932498, -12.41253812416062985, 4.000000000000000000 ) ) ;
#94530=DIRECTION ( 'NONE',  ( -0.000000000000000000, -0.000000000000000000, 1.000000000000000000 ) ) ;
#94532=ORIENTED_EDGE ( 'NONE', *, *, #90760, .T. ) ;
#94534=DIRECTION ( 'NONE',  ( -0.000000000000000000, -0.3543493200069152693, 0.9351131265310292928 ) ) ;
#94535=CARTESIAN_POINT ( 'NONE',  ( 66.29974487139159578, -27.71228299555252406, 4.000000000000000000 ) ) ;
#94537=LINE ( 'NONE', #129312, #87805 ) ;
#94538=VERTEX_POINT ( 'NONE', #55632 ) ;
#94539=EDGE_CURVE ( 'NONE', #474, #12595, #91131, .T. ) ;
#94540=ORIENTED_EDGE ( 'NONE', *, *, #9687, .T. ) ;
#94541=CARTESIAN_POINT ( 'NONE',  ( 39.29974487139159578, -27.71228299555233576, 4.000000000000000000 ) ) ;
#94542=ADVANCED_FACE ( 'NONE', ( #80255 ), #68661, .F. ) ;
#94543=DIRECTION ( 'NONE',  ( 0.7071067811865487940, 0.7071067811865463515, -0.000000000000000000 ) ) ;
#94544=CARTESIAN_POINT ( 'NONE',  ( -0.4616035537057042171, -9.740707523384180888, 17.74957260769610556 ) ) ;
#94545=FACE_OUTER_BOUND ( 'NONE', #115254, .T. ) ;
#94547=ORIENTED_EDGE ( 'NONE', *, *, #103061, .F. ) ;
#94548=VERTEX_POINT ( 'NONE', #111414 ) ;
#94549=VECTOR ( 'NONE', #45145, 1000.000000000000000 ) ;
#94550=FACE_OUTER_BOUND ( 'NONE', #86680, .T. ) ;
#94552=ORIENTED_EDGE ( 'NONE', *, *, #103217, .T. ) ;
#94554=EDGE_CURVE ( 'NONE', #1418, #27121, #12098, .T. ) ;
#94555=ORIENTED_EDGE ( 'NONE', *, *, #125066, .F. ) ;
#94556=VECTOR ( 'NONE', #41187, 1000.000000000000000 ) ;
#94557=DIRECTION ( 'NONE',  ( -0.3543493200069162685, -0.000000000000000000, -0.9351131265310288487 ) ) ;
#94559=DIRECTION ( 'NONE',  ( 0.7071067811865486830, -0.7071067811865464625, -0.000000000000000000 ) ) ;
#94560=CARTESIAN_POINT ( 'NONE',  ( 24.18398860626899705, 28.73617430169804265, 5.000000000000000000 ) ) ;
#94563=EDGE_CURVE ( 'NONE', #132778, #110801, #133897, .T. ) ;
#94564=FACE_BOUND ( 'NONE', #109394, .T. ) ;
#94565=EDGE_CURVE ( 'NONE', #120820, #22653, #61385, .T. ) ;
#94566=DIRECTION ( 'NONE',  ( 0.3543493200069162685, -0.000000000000000000, -0.9351131265310288487 ) ) ;
#94569=ORIENTED_EDGE ( 'NONE', *, *, #78248, .T. ) ;
#94572=EDGE_CURVE ( 'NONE', #98820, #26598, #27993, .T. ) ;
#94573=ORIENTED_EDGE ( 'NONE', *, *, #15629, .T. ) ;
#94574=EDGE_LOOP ( 'NONE', ( #100859, #15500, #68183, #91416 ) ) ;
#94577=DIRECTION ( 'NONE',  ( 0.7071067811865487940, -0.7071067811865463515, 0.000000000000000000 ) ) ;
#94578=CARTESIAN_POINT ( 'NONE',  ( 53.99451991528749062, 28.92564299267975869, 4.000000000000000000 ) ) ;
#94579=ADVANCED_FACE ( 'NONE', ( #59234 ), #59921, .F. ) ;
#94581=DIRECTION ( 'NONE',  ( 0.7071067811865486830, -0.7071067811865464625, -0.000000000000000000 ) ) ;
#94583=CARTESIAN_POINT ( 'NONE',  ( 21.18398860626899349, 28.73617430169802134, 5.000000000000000000 ) ) ;
#94584=VERTEX_POINT ( 'NONE', #103382 ) ;
#94585=CARTESIAN_POINT ( 'NONE',  ( 11.81601139373100651, 28.73617430169779041, 5.000000000000000000 ) ) ;
#94587=PLANE ( 'NONE',  #115186 ) ;
#94589=CARTESIAN_POINT ( 'NONE',  ( 25.78501580275793970, -3.740707523384241728, 15.76143240460129924 ) ) ;
#94590=LINE ( 'NONE', #57913, #58574 ) ;
#94591=CARTESIAN_POINT ( 'NONE',  ( 30.48921356237309510, -27.52281430457076894, 5.000000000000000000 ) ) ;
#94592=EDGE_CURVE ( 'NONE', #91502, #122835, #48312, .T. ) ;
#94593=LINE ( 'NONE', #82325, #12176 ) ;
#94594=ORIENTED_EDGE ( 'NONE', *, *, #78212, .T. ) ;
#94595=PLANE ( 'NONE',  #51922 ) ;
#94596=DIRECTION ( 'NONE',  ( 0.6830127018922180770, -0.6830127018922204085, -0.2588190451025213501 ) ) ;
#94597=VERTEX_POINT ( 'NONE', #50467 ) ;
#94598=ORIENTED_EDGE ( 'NONE', *, *, #117622, .T. ) ;
#94599=ORIENTED_EDGE ( 'NONE', *, *, #61517, .T. ) ;
#94600=EDGE_CURVE ( 'NONE', #53640, #100336, #125892, .T. ) ;
#94602=EDGE_CURVE ( 'NONE', #50248, #71285, #83091, .T. ) ;
#94603=ORIENTED_EDGE ( 'NONE', *, *, #115269, .F. ) ;
#94607=VERTEX_POINT ( 'NONE', #136736 ) ;
#94608=FACE_OUTER_BOUND ( 'NONE', #130705, .T. ) ;
#94609=EDGE_LOOP ( 'NONE', ( #86961, #88628, #103075 ) ) ;
#94610=LINE ( 'NONE', #129384, #88138 ) ;
#94611=LINE ( 'NONE', #128688, #121558 ) ;
#94612=LINE ( 'NONE', #29360, #10001 ) ;
#94613=ORIENTED_EDGE ( 'NONE', *, *, #83670, .F. ) ;
#94615=PLANE ( 'NONE',  #74675 ) ;
#94616=CARTESIAN_POINT ( 'NONE',  ( 31.49999999999978684, -17.56887692260763956, 4.000000000000000000 ) ) ;
#94617=VERTEX_POINT ( 'NONE', #6902 ) ;
#94618=CARTESIAN_POINT ( 'NONE',  ( 31.49999999999977973, -4.533600742197683608, 5.000000000000000000 ) ) ;
#94619=ORIENTED_EDGE ( 'NONE', *, *, #121990, .F. ) ;
#94620=EDGE_LOOP ( 'NONE', ( #26652, #120200, #141157, #128896 ) ) ;
#94622=ORIENTED_EDGE ( 'NONE', *, *, #20299, .F. ) ;
#94623=CARTESIAN_POINT ( 'NONE',  ( -6.299744871391586898, -27.71228299555210484, 4.000000000000000000 ) ) ;
#94624=AXIS2_PLACEMENT_3D ( 'NONE', #103668, #98867, #121340 ) ;
#94625=VECTOR ( 'NONE', #15616, 1000.000000000000000 ) ;
#94626=AXIS2_PLACEMENT_3D ( 'NONE', #92073, #13078, #101528 ) ;
#94628=VECTOR ( 'NONE', #64458, 1000.000000000000000 ) ;
#94629=DIRECTION ( 'NONE',  ( 0.7071067811865486830, -0.7071067811865464625, -0.000000000000000000 ) ) ;
#94630=LINE ( 'NONE', #62048, #143242 ) ;
#94631=VERTEX_POINT ( 'NONE', #127293 ) ;
#94632=PLANE ( 'NONE',  #27963 ) ;
#94633=ORIENTED_EDGE ( 'NONE', *, *, #74970, .F. ) ;
#94635=CARTESIAN_POINT ( 'NONE',  ( 1.171830600776465392, 18.75929247661552779, 4.000000000000000000 ) ) ;
#94639=DIRECTION ( 'NONE',  ( 0.6830127018922180770, -0.6830127018922204085, -0.2588190451025213501 ) ) ;
#94640=LINE ( 'NONE', #82375, #74464 ) ;
#94641=ORIENTED_EDGE ( 'NONE', *, *, #38003, .T. ) ;
#94642=EDGE_LOOP ( 'NONE', ( #114551, #26339, #47850, #21395 ) ) ;
#94643=EDGE_LOOP ( 'NONE', ( #33339, #117243, #140464, #7219, #110239 ) ) ;
#94644=LINE ( 'NONE', #27982, #20881 ) ;
#94645=DIRECTION ( 'NONE',  ( 0.7071067811865487940, -0.7071067811865463515, 0.000000000000000000 ) ) ;
#94646=CARTESIAN_POINT ( 'NONE',  ( -26.99451991528749417, 28.92564299267956685, 4.000000000000000000 ) ) ;
#94647=VECTOR ( 'NONE', #127673, 1000.000000000000000 ) ;
#94653=CARTESIAN_POINT ( 'NONE',  ( -51.48921356237309510, -27.52281430457091460, 5.000000000000000000 ) ) ;
#94655=CARTESIAN_POINT ( 'NONE',  ( 23.99999999999983302, 19.55218569542896390, 5.000000000000000000 ) ) ;
#94656=ORIENTED_EDGE ( 'NONE', *, *, #108227, .T. ) ;
#94657=DIRECTION ( 'NONE',  ( 0.7071067811865487940, 0.7071067811865463515, 0.000000000000000000 ) ) ;
#94658=ORIENTED_EDGE ( 'NONE', *, *, #80918, .F. ) ;
#94659=VECTOR ( 'NONE', #13160, 1000.000000000000227 ) ;
#94661=CARTESIAN_POINT ( 'NONE',  ( -6.299744871391586898, -27.71228299555210484, 4.000000000000000000 ) ) ;
#94662=LINE ( 'NONE', #93962, #62682 ) ;
#94664=EDGE_CURVE ( 'NONE', #127365, #52144, #26564, .T. ) ;
#94665=CARTESIAN_POINT ( 'NONE',  ( -2.939889289559783681, -9.740707523384180888, 10.89222023123381788 ) ) ;
#94666=DIRECTION ( 'NONE',  ( 0.6830127018922181881, 0.6830127018922202975, -0.2588190451025214056 ) ) ;
#94668=EDGE_CURVE ( 'NONE', #23904, #45259, #38170, .T. ) ;
#94669=ORIENTED_EDGE ( 'NONE', *, *, #16840, .F. ) ;
#94672=VECTOR ( 'NONE', #118004, 1000.000000000000227 ) ;
#94673=CARTESIAN_POINT ( 'NONE',  ( -33.79333936457824450, 21.75929247661549581, 4.998822639870701856 ) ) ;
#94675=CARTESIAN_POINT ( 'NONE',  ( -12.87485380690758063, -14.24070752338413648, 9.401115078912688716 ) ) ;
#94676=VERTEX_POINT ( 'NONE', #116431 ) ;
#94677=EDGE_CURVE ( 'NONE', #49642, #103979, #104089, .T. ) ;
#94678=DIRECTION ( 'NONE',  ( 0.3543493200069164351, 2.781805975412904658E-17, -0.9351131265310288487 ) ) ;
#94679=CARTESIAN_POINT ( 'NONE',  ( 15.48921356237309510, -27.52281430457066236, 5.000000000000000000 ) ) ;
#94682=CARTESIAN_POINT ( 'NONE',  ( -18.00548008471250583, 28.92564299267925776, 4.000000000000000000 ) ) ;
#94683=ORIENTED_EDGE ( 'NONE', *, *, #22513, .T. ) ;
#94685=DIRECTION ( 'NONE',  ( -0.7071067811865487940, 0.7071067811865463515, 0.000000000000000000 ) ) ;
#94688=LINE ( 'NONE', #86712, #59354 ) ;
#94689=DIRECTION ( 'NONE',  ( -1.000000000000000000, 0.000000000000000000, 0.000000000000000000 ) ) ;
#94690=LINE ( 'NONE', #20514, #119572 ) ;
#94691=ORIENTED_EDGE ( 'NONE', *, *, #32857, .T. ) ;
#94692=EDGE_CURVE ( 'NONE', #108003, #97591, #80956, .T. ) ;
#94694=FACE_OUTER_BOUND ( 'NONE', #81994, .T. ) ;
#94695=FACE_OUTER_BOUND ( 'NONE', #18496, .T. ) ;
#94696=DIRECTION ( 'NONE',  ( -0.000000000000000000, 1.000000000000000000, -0.000000000000000000 ) ) ;
#94697=EDGE_LOOP ( 'NONE', ( #85245, #8530, #112945, #46781 ) ) ;
#94698=DIRECTION ( 'NONE',  ( -0.6830127018922181881, 0.6830127018922202975, -0.2588190451025214056 ) ) ;
#94699=CARTESIAN_POINT ( 'NONE',  ( -22.82900182742193351, 7.795401085224272109, 5.000000000000000000 ) ) ;
#94702=ORIENTED_EDGE ( 'NONE', *, *, #57413, .T. ) ;
#94703=EDGE_LOOP ( 'NONE', ( #38148, #78471, #7904, #121428 ) ) ;
#94705=ORIENTED_EDGE ( 'NONE', *, *, #82453, .T. ) ;
#94706=CARTESIAN_POINT ( 'NONE',  ( -24.48921356237309510, -27.52281430457072631, 5.000000000000000000 ) ) ;
#94707=EDGE_CURVE ( 'NONE', #130915, #97535, #5498, .T. ) ;
#94708=CARTESIAN_POINT ( 'NONE',  ( -13.49999999999990763, 22.22500000000000142, 4.362957392718799454 ) ) ;
#94709=DIRECTION ( 'NONE',  ( 0.7071067811865486830, -0.7071067811865464625, -0.000000000000000000 ) ) ;
#94710=ORIENTED_EDGE ( 'NONE', *, *, #23206, .F. ) ;
#94711=DIRECTION ( 'NONE',  ( -0.7071067811865487940, 0.7071067811865463515, -0.000000000000000000 ) ) ;
#94714=EDGE_CURVE ( 'NONE', #140579, #72813, #60668, .T. ) ;
#94715=ORIENTED_EDGE ( 'NONE', *, *, #4622, .T. ) ;
#94716=LINE ( 'NONE', #83910, #116076 ) ;
#94717=LINE ( 'NONE', #81771, #94127 ) ;
#94718=DIRECTION ( 'NONE',  ( 0.6830127018922181881, 0.6830127018922202975, -0.2588190451025214056 ) ) ;
#94720=VECTOR ( 'NONE', #39416, 999.9999999999998863 ) ;
#94721=VECTOR ( 'NONE', #122908, 1000.000000000000000 ) ;
#94722=ADVANCED_FACE ( 'NONE', ( #72967 ), #117124, .T. ) ;
#94723=ORIENTED_EDGE ( 'NONE', *, *, #80787, .F. ) ;
#94724=VERTEX_POINT ( 'NONE', #62783 ) ;
#94726=EDGE_CURVE ( 'NONE', #140742, #53886, #96765, .T. ) ;
#94727=EDGE_CURVE ( 'NONE', #111382, #98928, #85937, .T. ) ;
#94728=CARTESIAN_POINT ( 'NONE',  ( -60.48921356237309510, -27.52281430457097500, 5.000000000000000000 ) ) ;
#94729=PLANE ( 'NONE',  #13781 ) ;
#94731=CARTESIAN_POINT ( 'NONE',  ( -21.48921356237309155, -27.52281430457070499, 5.000000000000000000 ) ) ;
#94732=DIRECTION ( 'NONE',  ( -1.000000000000000000, 0.000000000000000000, -0.000000000000000000 ) ) ;
#94733=CARTESIAN_POINT ( 'NONE',  ( 0.000000000000000000, 0.000000000000000000, 5.000000000000000000 ) ) ;
#94734=EDGE_LOOP ( 'NONE', ( #131493, #98978, #139881, #42690 ) ) ;
#94736=ORIENTED_EDGE ( 'NONE', *, *, #56229, .T. ) ;
#94737=EDGE_CURVE ( 'NONE', #76243, #81473, #130175, .T. ) ;
#94739=ORIENTED_EDGE ( 'NONE', *, *, #85299, .T. ) ;
#94740=AXIS2_PLACEMENT_3D ( 'NONE', #88278, #142648, #132526 ) ;
#94741=AXIS2_PLACEMENT_3D ( 'NONE', #41570, #30729, #47685 ) ;
#94742=EDGE_CURVE ( 'NONE', #13302, #22212, #131593, .T. ) ;
#94744=AXIS2_PLACEMENT_3D ( 'NONE', #9633, #19808, #62628 ) ;
#94745=LINE ( 'NONE', #137572, #126148 ) ;
#94746=ORIENTED_EDGE ( 'NONE', *, *, #69908, .T. ) ;
#94748=DIRECTION ( 'NONE',  ( 0.6830127018922180770, -0.6830127018922204085, -0.2588190451025213501 ) ) ;
#94749=DIRECTION ( 'NONE',  ( 0.3543493200069162685, -0.000000000000000000, -0.9351131265310288487 ) ) ;
#94750=DIRECTION ( 'NONE',  ( -0.7071067811865486830, -0.7071067811865464625, 0.000000000000000000 ) ) ;
#94751=VECTOR ( 'NONE', #86552, 1000.000000000000000 ) ;
#94753=VERTEX_POINT ( 'NONE', #75792 ) ;
#94755=CARTESIAN_POINT ( 'NONE',  ( 2.207106781186527478, -5.240707523384232402, 5.000000000000000000 ) ) ;
#94756=DIRECTION ( 'NONE',  ( 0.7071067811865486830, -0.7071067811865464625, -0.000000000000000000 ) ) ;
#94757=AXIS2_PLACEMENT_3D ( 'NONE', #21763, #10157, #97896 ) ;
#94758=VERTEX_POINT ( 'NONE', #109833 ) ;
#94759=DIRECTION ( 'NONE',  ( 0.7071067811865486830, -0.7071067811865464625, -0.000000000000000000 ) ) ;
#94761=CARTESIAN_POINT ( 'NONE',  ( 17.92867102513379862, 9.037728232668255757, 5.000000000000000000 ) ) ;
#94762=VECTOR ( 'NONE', #55897, 1000.000000000000000 ) ;
#94763=EDGE_LOOP ( 'NONE', ( #142157, #94555, #137529, #98942 ) ) ;
#94764=ORIENTED_EDGE ( 'NONE', *, *, #75095, .T. ) ;
#94766=VECTOR ( 'NONE', #116455, 1000.000000000000000 ) ;
#94767=ORIENTED_EDGE ( 'NONE', *, *, #136171, .F. ) ;
#94770=CARTESIAN_POINT ( 'NONE',  ( -34.42500000000001137, -18.02281430457038880, 5.000000000000000000 ) ) ;
#94771=EDGE_CURVE ( 'NONE', #21869, #119070, #86671, .T. ) ;
#94772=CARTESIAN_POINT ( 'NONE',  ( 23.29387692260788967, 22.22500000000000142, 4.000000000000000000 ) ) ;
#94774=DIRECTION ( 'NONE',  ( -0.000000000000000000, 0.3543493200069152138, -0.9351131265310292928 ) ) ;
#94775=PLANE ( 'NONE',  #113837 ) ;
#94776=CARTESIAN_POINT ( 'NONE',  ( 42.48921356237308800, -27.52281430457085065, 5.000000000000000000 ) ) ;
#94778=ADVANCED_FACE ( 'NONE', ( #106966 ), #20667, .T. ) ;
#94779=PLANE ( 'NONE',  #100256 ) ;
#94780=CARTESIAN_POINT ( 'NONE',  ( 23.67183060077631396, 17.25929247661554555, 4.000000000000000000 ) ) ;
#94781=EDGE_LOOP ( 'NONE', ( #117050, #4733, #105801, #74886, #132315 ) ) ;
#94782=CARTESIAN_POINT ( 'NONE',  ( -51.18398860626899705, 28.73617430169823095, 5.000000000000000000 ) ) ;
#94783=EDGE_LOOP ( 'NONE', ( #9116, #86281, #134170, #45778 ) ) ;
#94784=ORIENTED_EDGE ( 'NONE', *, *, #96786, .T. ) ;
#94785=VERTEX_POINT ( 'NONE', #130899 ) ;
#94786=DIRECTION ( 'NONE',  ( -0.000000000000000000, 0.3543493200069153248, 0.9351131265310292928 ) ) ;
#94788=DIRECTION ( 'NONE',  ( 1.000000000000000000, 0.000000000000000000, 0.000000000000000000 ) ) ;
#94791=VERTEX_POINT ( 'NONE', #7645 ) ;
#94793=ORIENTED_EDGE ( 'NONE', *, *, #110002, .F. ) ;
#94795=CARTESIAN_POINT ( 'NONE',  ( 34.92499999999998295, -15.18334561358938650, 4.500000000000000888 ) ) ;
#94796=DIRECTION ( 'NONE',  ( -0.7071067811865486830, -0.7071067811865464625, 0.000000000000000000 ) ) ;
#94797=CARTESIAN_POINT ( 'NONE',  ( 22.49999999999984723, -2.947814304570794075, 5.000000000000000000 ) ) ;
#94798=ORIENTED_EDGE ( 'NONE', *, *, #133295, .F. ) ;
#94799=ORIENTED_EDGE ( 'NONE', *, *, #137370, .T. ) ;
#94800=VERTEX_POINT ( 'NONE', #139646 ) ;
#94801=CARTESIAN_POINT ( 'NONE',  ( 26.99999999999981526, -19.22509904557633931, 1.855685503482240373 ) ) ;
#94802=DIRECTION ( 'NONE',  ( -0.6830127018922181881, 0.6830127018922202975, -0.2588190451025214056 ) ) ;
#94803=DIRECTION ( 'NONE',  ( -0.7071067811865487940, 0.7071067811865463515, -0.000000000000000000 ) ) ;
#94804=DIRECTION ( 'NONE',  ( -0.6830127018922180770, -0.6830127018922204085, -0.2588190451025213501 ) ) ;
#94805=DIRECTION ( 'NONE',  ( -0.7071067811865486830, 0.7071067811865464625, 0.000000000000000000 ) ) ;
#94806=DIRECTION ( 'NONE',  ( 0.6830127018922181881, 0.6830127018922202975, -0.2588190451025214056 ) ) ;
#94807=EDGE_CURVE ( 'NONE', #23195, #23765, #128729, .T. ) ;
#94808=LINE ( 'NONE', #139073, #2231 ) ;
#94812=VECTOR ( 'NONE', #74693, 1000.000000000000227 ) ;
#94813=VECTOR ( 'NONE', #106951, 1000.000000000000000 ) ;
#94815=CARTESIAN_POINT ( 'NONE',  ( -34.42500000000001137, 21.72500000000000142, 0.4999999999999995559 ) ) ;
#94818=ADVANCED_FACE ( 'NONE', ( #85209 ), #9034, .F. ) ;
#94819=DIRECTION ( 'NONE',  ( 0.7071067811865487940, 0.7071067811865463515, -0.000000000000000000 ) ) ;
#94820=PLANE ( 'NONE',  #34953 ) ;
#94821=ORIENTED_EDGE ( 'NONE', *, *, #110122, .F. ) ;
#94822=EDGE_CURVE ( 'NONE', #139864, #141891, #52588, .T. ) ;
#94823=CARTESIAN_POINT ( 'NONE',  ( 8.999999999999944933, 11.96639925780214675, 5.000000000000000000 ) ) ;
#94825=ORIENTED_EDGE ( 'NONE', *, *, #43465, .F. ) ;
#94826=LINE ( 'NONE', #4206, #9540 ) ;
#94827=VECTOR ( 'NONE', #17975, 999.9999999999998863 ) ;
#94828=VERTEX_POINT ( 'NONE', #109107 ) ;
#94829=EDGE_CURVE ( 'NONE', #118847, #38733, #120686, .T. ) ;
#94830=EDGE_CURVE ( 'NONE', #38833, #80915, #26919, .T. ) ;
#94831=CARTESIAN_POINT ( 'NONE',  ( 34.92499999999998295, -20.99387692260782501, 4.000000000000000000 ) ) ;
#94835=LINE ( 'NONE', #7098, #69133 ) ;
#94836=EDGE_CURVE ( 'NONE', #90375, #59049, #25477, .T. ) ;
#94837=CARTESIAN_POINT ( 'NONE',  ( 19.19018167574436262, -18.74070752338409562, 7.910009926591462737 ) ) ;
#94838=FACE_OUTER_BOUND ( 'NONE', #135600, .T. ) ;
#94839=LINE ( 'NONE', #60123, #110800 ) ;
#94842=VECTOR ( 'NONE', #16025, 1000.000000000000000 ) ;
#94845=DIRECTION ( 'NONE',  ( -0.7071067811865486830, 0.7071067811865464625, 0.000000000000000000 ) ) ;
#94846=CARTESIAN_POINT ( 'NONE',  ( 6.792893218813414791, -5.240707523384228850, 5.000000000000000000 ) ) ;
#94847=ORIENTED_EDGE ( 'NONE', *, *, #15070, .T. ) ;
#94848=( BOUNDED_CURVE ( )  B_SPLINE_CURVE ( 3, ( #77377, #85339, #132479, #31003 ),
 .UNSPECIFIED., .F., .F. ) 
 B_SPLINE_CURVE_WITH_KNOTS ( ( 4, 4 ),
 ( 2.001653308786174090, 3.503810798801451742 ),
 .UNSPECIFIED. ) 
 CURVE ( )  GEOMETRIC_REPRESENTATION_ITEM ( )  RATIONAL_B_SPLINE_CURVE ( ( 1.000000000000000000, 0.8206354192515249446, 0.8206354192515249446, 1.000000000000000000 ) ) 
 REPRESENTATION_ITEM ( '' )  );
#94849=VERTEX_POINT ( 'NONE', #67055 ) ;
#94851=EDGE_CURVE ( 'NONE', #133319, #69181, #11188, .T. ) ;
#94852=VECTOR ( 'NONE', #54803, 1000.000000000000000 ) ;
#94856=PLANE ( 'NONE',  #23230 ) ;
#94857=DIRECTION ( 'NONE',  ( 0.6830127018922180770, -0.6830127018922204085, -0.2588190451025213501 ) ) ;
#94858=ORIENTED_EDGE ( 'NONE', *, *, #77584, .T. ) ;
#94859=AXIS2_PLACEMENT_3D ( 'NONE', #52630, #22136, #9844 ) ;
#94860=EDGE_CURVE ( 'NONE', #96026, #142433, #77244, .T. ) ;
#94861=CARTESIAN_POINT ( 'NONE',  ( -34.92500000000001137, 22.22500000000000142, 4.000000000000000000 ) ) ;
#94862=DIRECTION ( 'NONE',  ( 0.7071067811865487940, 0.7071067811865463515, -0.000000000000000000 ) ) ;
#94863=VECTOR ( 'NONE', #59420, 1000.000000000000000 ) ;
#94865=DIRECTION ( 'NONE',  ( 2.781805975412905274E-17, -0.3543493200069152138, 0.9351131265310292928 ) ) ;
#94866=AXIS2_PLACEMENT_3D ( 'NONE', #5789, #4319, #92825 ) ;
#94867=CARTESIAN_POINT ( 'NONE',  ( 21.18398860626899349, 28.73617430169802134, 5.000000000000000000 ) ) ;
#94868=CARTESIAN_POINT ( 'NONE',  ( -24.25645252394784990, 6.095695649681008632, 4.664440252871067116 ) ) ;
#94869=CARTESIAN_POINT ( 'NONE',  ( 15.48921356237309510, -27.52281430457066236, 5.000000000000000000 ) ) ;
#94871=DIRECTION ( 'NONE',  ( 0.7071067811865486830, -0.7071067811865464625, -0.000000000000000000 ) ) ;
#94872=DIRECTION ( 'NONE',  ( -0.6830127018922180770, -0.6830127018922204085, -0.2588190451025213501 ) ) ;
#94874=CARTESIAN_POINT ( 'NONE',  ( -33.70710678118631165, -3.740707523384248390, 5.000000000000000000 ) ) ;
#94876=ORIENTED_EDGE ( 'NONE', *, *, #32331, .T. ) ;
#94877=ORIENTED_EDGE ( 'NONE', *, *, #88567, .T. ) ;
#94879=EDGE_LOOP ( 'NONE', ( #82017, #131706, #48907, #39162 ) ) ;
#94880=EDGE_CURVE ( 'NONE', #86612, #121778, #89507, .T. ) ;
#94882=AXIS2_PLACEMENT_3D ( 'NONE', #63526, #27439, #96781 ) ;
#94883=DIRECTION ( 'NONE',  ( -0.7071067811865486830, -0.7071067811865464625, -0.000000000000000000 ) ) ;
#94884=ORIENTED_EDGE ( 'NONE', *, *, #139592, .T. ) ;
#94885=FACE_OUTER_BOUND ( 'NONE', #117604, .T. ) ;
#94886=CARTESIAN_POINT ( 'NONE',  ( 0.000000000000000000, 0.000000000000000000, 5.000000000000000000 ) ) ;
#94887=ADVANCED_FACE ( 'NONE', ( #103064 ), #71168, .F. ) ;
#94889=ORIENTED_EDGE ( 'NONE', *, *, #18942, .T. ) ;
#94890=EDGE_CURVE ( 'NONE', #17479, #91909, #92889, .T. ) ;
#94891=LINE ( 'NONE', #52124, #4890 ) ;
#94892=ORIENTED_EDGE ( 'NONE', *, *, #21743, .T. ) ;
#94893=LINE ( 'NONE', #72962, #54608 ) ;
#94894=DIRECTION ( 'NONE',  ( -0.7071067811865487940, 0.7071067811865463515, -0.000000000000000000 ) ) ;
#94895=VECTOR ( 'NONE', #114059, 1000.000000000000000 ) ;
#94900=ORIENTED_EDGE ( 'NONE', *, *, #5322, .T. ) ;
#94901=VERTEX_POINT ( 'NONE', #44626 ) ;
#94902=FACE_OUTER_BOUND ( 'NONE', #68643, .T. ) ;
#94903=DIRECTION ( 'NONE',  ( -0.7071067811865486830, -0.7071067811865464625, 0.000000000000000000 ) ) ;
#94905=VECTOR ( 'NONE', #57805, 1000.000000000000227 ) ;
#94906=VECTOR ( 'NONE', #5822, 999.9999999999998863 ) ;
#94907=CARTESIAN_POINT ( 'NONE',  ( 10.82816939922345156, -8.240707523384200428, 4.000000000000000000 ) ) ;
#94909=ORIENTED_EDGE ( 'NONE', *, *, #117550, .T. ) ;
#94910=ORIENTED_EDGE ( 'NONE', *, *, #55465, .F. ) ;
#94911=EDGE_CURVE ( 'NONE', #118679, #111906, #43876, .T. ) ;
#94912=PLANE ( 'NONE',  #89692 ) ;
#94913=VERTEX_POINT ( 'NONE', #22093 ) ;
#94914=ORIENTED_EDGE ( 'NONE', *, *, #108705, .T. ) ;
#94915=EDGE_CURVE ( 'NONE', #22337, #12371, #36382, .T. ) ;
#94917=AXIS2_PLACEMENT_3D ( 'NONE', #40462, #116570, #94788 ) ;
#94918=LINE ( 'NONE', #104372, #67698 ) ;
#94920=VERTEX_POINT ( 'NONE', #133047 ) ;
#94921=CARTESIAN_POINT ( 'NONE',  ( 5.999999999999960032, -3.485240976185074224, -4.108735105802382215 ) ) ;
#94922=VECTOR ( 'NONE', #24142, 999.9999999999998863 ) ;
#94923=DIRECTION ( 'NONE',  ( 0.7071067811865487940, 0.7071067811865463515, 0.000000000000000000 ) ) ;
#94924=VECTOR ( 'NONE', #81112, 1000.000000000000000 ) ;
#94925=CIRCLE ( 'NONE', #104232, 5.968999999999998529 ) ;
#94926=VECTOR ( 'NONE', #90570, 1000.000000000000000 ) ;
#94928=ORIENTED_EDGE ( 'NONE', *, *, #100153, .F. ) ;
#94929=DIRECTION ( 'NONE',  ( 0.3543493200069164351, 2.781805975412904658E-17, -0.9351131265310288487 ) ) ;
#94930=FACE_BOUND ( 'NONE', #119627, .T. ) ;
#94931=ORIENTED_EDGE ( 'NONE', *, *, #43077, .F. ) ;
#94932=CARTESIAN_POINT ( 'NONE',  ( 21.18398860626899349, 28.73617430169802134, 5.000000000000000000 ) ) ;
#94933=DIRECTION ( 'NONE',  ( 0.7071067811865487940, -0.7071067811865463515, 0.000000000000000000 ) ) ;
#94934=CARTESIAN_POINT ( 'NONE',  ( 0.1839886062690032631, 28.73617430169787568, 5.000000000000000000 ) ) ;
#94935=ORIENTED_EDGE ( 'NONE', *, *, #78186, .F. ) ;
#94936=DIRECTION ( 'NONE',  ( 0.7071067811865486830, -0.7071067811865464625, -0.000000000000000000 ) ) ;
#94938=VERTEX_POINT ( 'NONE', #99654 ) ;
#94939=VERTEX_POINT ( 'NONE', #115312 ) ;
#94942=DIRECTION ( 'NONE',  ( 0.7071067811865486830, -0.7071067811865464625, -0.000000000000000000 ) ) ;
#94943=PLANE ( 'NONE',  #109682 ) ;
#94945=CARTESIAN_POINT ( 'NONE',  ( 11.29289321881338459, 5.259292476615667233, 5.000000000000000000 ) ) ;
#94946=FACE_OUTER_BOUND ( 'NONE', #12551, .T. ) ;
#94948=VECTOR ( 'NONE', #136237, 1000.000000000000000 ) ;
#94949=DIRECTION ( 'NONE',  ( -0.3543493200069162685, -0.000000000000000000, -0.9351131265310288487 ) ) ;
#94950=VECTOR ( 'NONE', #68542, 1000.000000000000000 ) ;
#94951=EDGE_CURVE ( 'NONE', #12119, #11674, #111239, .T. ) ;
#94952=LINE ( 'NONE', #117409, #138574 ) ;
#94953=FACE_OUTER_BOUND ( 'NONE', #33979, .T. ) ;
#94954=CARTESIAN_POINT ( 'NONE',  ( 17.99999999999987566, -15.41253812416059787, 4.000000000000000000 ) ) ;
#94955=ORIENTED_EDGE ( 'NONE', *, *, #65492, .F. ) ;
#94956=VECTOR ( 'NONE', #127887, 1000.000000000000000 ) ;
#94957=EDGE_LOOP ( 'NONE', ( #112995, #6859, #73870, #26111 ) ) ;
#94958=VERTEX_POINT ( 'NONE', #92162 ) ;
#94959=VERTEX_POINT ( 'NONE', #100400 ) ;
#94960=CARTESIAN_POINT ( 'NONE',  ( -23.99999999999983302, -7.068876922607743474, 4.000000000000000000 ) ) ;
#94961=ORIENTED_EDGE ( 'NONE', *, *, #138854, .T. ) ;
#94963=VERTEX_POINT ( 'NONE', #14621 ) ;
#94964=FACE_OUTER_BOUND ( 'NONE', #142749, .T. ) ;
#94965=ADVANCED_FACE ( 'NONE', ( #136391 ), #37081, .F. ) ;
#94967=ORIENTED_EDGE ( 'NONE', *, *, #100826, .T. ) ;
#94968=PLANE ( 'NONE',  #32529 ) ;
#94969=EDGE_LOOP ( 'NONE', ( #122055, #119829, #3465, #109811 ) ) ;
#94970=DIRECTION ( 'NONE',  ( 0.7071067811865486830, -0.7071067811865464625, -0.000000000000000000 ) ) ;
#94971=CARTESIAN_POINT ( 'NONE',  ( 34.75611968250419181, 8.812934254707293746, 4.955485411084883829 ) ) ;
#94973=ORIENTED_EDGE ( 'NONE', *, *, #55889, .T. ) ;
#94975=CARTESIAN_POINT ( 'NONE',  ( 16.11017322888198677, -22.22500000000000497, 4.785647885939352086 ) ) ;
#94977=VERTEX_POINT ( 'NONE', #59580 ) ;
#94978=VERTEX_POINT ( 'NONE', #103741 ) ;
#94980=AXIS2_PLACEMENT_3D ( 'NONE', #26244, #112527, #49453 ) ;
#94981=VERTEX_POINT ( 'NONE', #4384 ) ;
#94982=DIRECTION ( 'NONE',  ( -0.7071067811865487940, 0.7071067811865463515, 0.000000000000000000 ) ) ;
#94983=PLANE ( 'NONE',  #104320 ) ;
#94984=PLANE ( 'NONE',  #33102 ) ;
#94987=CARTESIAN_POINT ( 'NONE',  ( -5.999999999999960920, 19.55218569542897100, 5.000000000000000000 ) ) ;
#94988=DIRECTION ( 'NONE',  ( -0.6830127018922181881, 0.6830127018922202975, -0.2588190451025214056 ) ) ;
#94989=LINE ( 'NONE', #139265, #67406 ) ;
#94991=VERTEX_POINT ( 'NONE', #93617 ) ;
#94993=AXIS2_PLACEMENT_3D ( 'NONE', #81287, #2973, #93570 ) ;
#94994=CARTESIAN_POINT ( 'NONE',  ( 15.48921356237309510, -27.52281430457066236, 5.000000000000000000 ) ) ;
#94995=VERTEX_POINT ( 'NONE', #39243 ) ;
#94996=LINE ( 'NONE', #5837, #115709 ) ;
#94997=ORIENTED_EDGE ( 'NONE', *, *, #12871, .F. ) ;
#94998=EDGE_CURVE ( 'NONE', #54275, #88406, #126929, .T. ) ;
#95000=ORIENTED_EDGE ( 'NONE', *, *, #40757, .T. ) ;
#95001=CARTESIAN_POINT ( 'NONE',  ( 34.75611968250419181, -12.18706574529247710, 4.955485411084880276 ) ) ;
#95002=LINE ( 'NONE', #82051, #85435 ) ;
#95003=AXIS2_PLACEMENT_3D ( 'NONE', #128055, #37467, #93964 ) ;
#95006=EDGE_CURVE ( 'NONE', #57200, #25994, #50117, .T. ) ;
#95007=EDGE_CURVE ( 'NONE', #139559, #116329, #127681, .T. ) ;
#95008=LINE ( 'NONE', #71884, #116895 ) ;
#95009=EDGE_CURVE ( 'NONE', #56334, #22212, #95745, .T. ) ;
#95010=( BOUNDED_CURVE ( )  B_SPLINE_CURVE ( 3, ( #75712, #73569, #30037, #95301 ),
 .UNSPECIFIED., .F., .T. ) 
 B_SPLINE_CURVE_WITH_KNOTS ( ( 4, 4 ),
 ( 1.964434688349487423, 3.503810798801450854 ),
 .UNSPECIFIED. ) 
 CURVE ( )  GEOMETRIC_REPRESENTATION_ITEM ( )  RATIONAL_B_SPLINE_CURVE ( ( 1.000000000000000000, 0.8120851936182280628, 0.8120851936182280628, 1.000000000000000000 ) ) 
 REPRESENTATION_ITEM ( '' )  );
#95011=PLANE ( 'NONE',  #18377 ) ;
#95013=EDGE_CURVE ( 'NONE', #106292, #10266, #49427, .T. ) ;
#95015=CARTESIAN_POINT ( 'NONE',  ( -7.809818324255463295, -18.74070752338408852, 7.910009926591528462 ) ) ;
#95016=DIRECTION ( 'NONE',  ( -0.7071067811865486830, -0.7071067811865464625, -0.000000000000000000 ) ) ;
#95017=CARTESIAN_POINT ( 'NONE',  ( -9.299744871391588674, -27.71228299555212971, 4.000000000000000000 ) ) ;
#95020=VECTOR ( 'NONE', #39246, 999.9999999999998863 ) ;
#95021=LINE ( 'NONE', #85578, #28040 ) ;
#95022=EDGE_LOOP ( 'NONE', ( #73837, #135642, #90614, #29369 ) ) ;
#95023=ORIENTED_EDGE ( 'NONE', *, *, #95893, .F. ) ;
#95024=VERTEX_POINT ( 'NONE', #16757 ) ;
#95028=VECTOR ( 'NONE', #139538, 1000.000000000000000 ) ;
#95029=EDGE_LOOP ( 'NONE', ( #135280, #58310, #132096, #26934 ) ) ;
#95032=LINE ( 'NONE', #136406, #43300 ) ;
#95033=CARTESIAN_POINT ( 'NONE',  ( 45.29974487139158867, -27.71228299555237840, 4.000000000000000000 ) ) ;
#95034=VECTOR ( 'NONE', #137629, 1000.000000000000000 ) ;
#95035=VECTOR ( 'NONE', #17811, 1000.000000000000000 ) ;
#95036=AXIS2_PLACEMENT_3D ( 'NONE', #18673, #52740, #129586 ) ;
#95038=EDGE_LOOP ( 'NONE', ( #63342, #108174, #92266, #72929 ) ) ;
#95039=LINE ( 'NONE', #104496, #136475 ) ;
#95040=VECTOR ( 'NONE', #74323, 999.9999999999998863 ) ;
#95041=ADVANCED_FACE ( 'NONE', ( #29758 ), #72623, .F. ) ;
#95044=DIRECTION ( 'NONE',  ( 0.7071067811865487940, 0.7071067811865463515, 0.000000000000000000 ) ) ;
#95046=ORIENTED_EDGE ( 'NONE', *, *, #110496, .T. ) ;
#95049=CARTESIAN_POINT ( 'NONE',  ( -34.92500000000001137, 22.22500000000000142, 4.500000000000000888 ) ) ;
#95050=VECTOR ( 'NONE', #94159, 1000.000000000000000 ) ;
#95051=CARTESIAN_POINT ( 'NONE',  ( 7.499999999999954703, 16.08746187583908593, 4.000000000000000000 ) ) ;
#95053=ADVANCED_FACE ( 'NONE', ( #117472 ), #82745, .T. ) ;
#95054=CARTESIAN_POINT ( 'NONE',  ( 45.18398860626900415, 28.73617430169818832, 5.000000000000000000 ) ) ;
#95055=DIRECTION ( 'NONE',  ( 0.6830127018922180770, -0.6830127018922204085, -0.2588190451025213501 ) ) ;
#95058=CARTESIAN_POINT ( 'NONE',  ( 32.99999999999977263, -0.2811185226894025169, -5.995736974527589247 ) ) ;
#95059=ORIENTED_EDGE ( 'NONE', *, *, #90630, .F. ) ;
#95060=ORIENTED_EDGE ( 'NONE', *, *, #95853, .T. ) ;
#95062=VERTEX_POINT ( 'NONE', #41353 ) ;
#95063=LINE ( 'NONE', #84239, #27501 ) ;
#95064=AXIS2_PLACEMENT_3D ( 'NONE', #80260, #67977, #99840 ) ;
#95065=DIRECTION ( 'NONE',  ( 0.000000000000000000, -1.000000000000000000, 0.000000000000000000 ) ) ;
#95066=CARTESIAN_POINT ( 'NONE',  ( -36.18398860626899705, 28.73617430169812437, 5.000000000000000000 ) ) ;
#95068=CARTESIAN_POINT ( 'NONE',  ( 57.48921356237308800, -27.52281430457095368, 5.000000000000000000 ) ) ;
#95069=VECTOR ( 'NONE', #119664, 1000.000000000000227 ) ;
#95070=EDGE_CURVE ( 'NONE', #88325, #121941, #105190, .T. ) ;
#95071=VECTOR ( 'NONE', #127788, 1000.000000000000000 ) ;
#95073=ORIENTED_EDGE ( 'NONE', *, *, #100281, .T. ) ;
#95074=ADVANCED_FACE ( 'NONE', ( #5852 ), #63156, .F. ) ;
#95076=DIRECTION ( 'NONE',  ( -0.7071067811865487940, 0.7071067811865463515, 0.000000000000000000 ) ) ;
#95077=ORIENTED_EDGE ( 'NONE', *, *, #63811, .T. ) ;
#95078=CARTESIAN_POINT ( 'NONE',  ( 18.48921356237309510, -27.52281430457068367, 5.000000000000000000 ) ) ;
#95079=AXIS2_PLACEMENT_3D ( 'NONE', #323, #100399, #79400 ) ;
#95081=DIRECTION ( 'NONE',  ( -0.7071067811865486830, 0.7071067811865464625, 0.000000000000000000 ) ) ;
#95082=ADVANCED_FACE ( 'NONE', ( #83458 ), #94314, .F. ) ;
#95083=CARTESIAN_POINT ( 'NONE',  ( 40.04515773336642326, -21.74070752338406365, 21.72585301388593848 ) ) ;
#95084=ORIENTED_EDGE ( 'NONE', *, *, #132060, .F. ) ;
#95086=ORIENTED_EDGE ( 'NONE', *, *, #104739, .F. ) ;
#95087=FACE_OUTER_BOUND ( 'NONE', #67184, .T. ) ;
#95091=( BOUNDED_CURVE ( )  B_SPLINE_CURVE ( 3, ( #75651, #10360, #121976, #111090 ),
 .UNSPECIFIED., .F., .T. ) 
 B_SPLINE_CURVE_WITH_KNOTS ( ( 4, 4 ),
 ( 5.043186909253407180, 5.074607125596344304 ),
 .UNSPECIFIED. ) 
 CURVE ( )  GEOMETRIC_REPRESENTATION_ITEM ( )  RATIONAL_B_SPLINE_CURVE ( ( 1.000000000000000000, 0.9999177325257868620, 0.9999177325257868620, 1.000000000000000000 ) ) 
 REPRESENTATION_ITEM ( '' )  );
#95092=VECTOR ( 'NONE', #30120, 1000.000000000000000 ) ;
#95094=ORIENTED_EDGE ( 'NONE', *, *, #54570, .T. ) ;
#95095=DIRECTION ( 'NONE',  ( 1.000000000000000000, 0.000000000000000000, 0.000000000000000000 ) ) ;
#95096=ADVANCED_FACE ( 'NONE', ( #116782 ), #95011, .F. ) ;
#95097=LINE ( 'NONE', #73384, #80317 ) ;
#95099=VERTEX_POINT ( 'NONE', #52242 ) ;
#95100=AXIS2_PLACEMENT_3D ( 'NONE', #35559, #71023, #3564 ) ;
#95101=DIRECTION ( 'NONE',  ( 0.7071067811865487940, 0.7071067811865463515, 0.000000000000000000 ) ) ;
#95102=ORIENTED_EDGE ( 'NONE', *, *, #104059, .T. ) ;
#95103=CARTESIAN_POINT ( 'NONE',  ( 45.48921356237309510, -27.52281430457087197, 5.000000000000000000 ) ) ;
#95104=EDGE_CURVE ( 'NONE', #10011, #121745, #29069, .T. ) ;
#95105=EDGE_LOOP ( 'NONE', ( #35481, #111673, #77582, #107821 ) ) ;
#95108=PLANE ( 'NONE',  #23347 ) ;
#95109=ADVANCED_FACE ( 'NONE', ( #11558 ), #142825, .F. ) ;
#95110=FACE_BOUND ( 'NONE', #116372, .T. ) ;
#95111=DIRECTION ( 'NONE',  ( 0.7071067811865486830, -0.7071067811865464625, -0.000000000000000000 ) ) ;
#95113=DIRECTION ( 'NONE',  ( 0.7071067811865486830, -0.7071067811865464625, -0.000000000000000000 ) ) ;
#95114=ORIENTED_EDGE ( 'NONE', *, *, #63495, .F. ) ;
#95116=LINE ( 'NONE', #105973, #50478 ) ;
#95117=ORIENTED_EDGE ( 'NONE', *, *, #142380, .T. ) ;
#95118=VERTEX_POINT ( 'NONE', #66699 ) ;
#95119=VECTOR ( 'NONE', #68356, 1000.000000000000000 ) ;
#95120=CARTESIAN_POINT ( 'NONE',  ( 39.29974487139159578, -27.71228299555233576, 4.000000000000000000 ) ) ;
#95122=ADVANCED_FACE ( 'NONE', ( #89166 ), #131233, .T. ) ;
#95125=CARTESIAN_POINT ( 'NONE',  ( -1.171830600776458509, -11.24070752338416490, 4.000000000000000000 ) ) ;
#95126=EDGE_LOOP ( 'NONE', ( #6672, #33075, #5399, #138620 ) ) ;
#95127=PLANE ( 'NONE',  #14378 ) ;
#95128=VECTOR ( 'NONE', #11524, 1000.000000000000000 ) ;
#95129=ADVANCED_FACE ( 'NONE', ( #77593 ), #9408, .F. ) ;
#95130=VECTOR ( 'NONE', #22197, 1000.000000000000227 ) ;
#95131=VECTOR ( 'NONE', #111510, 999.9999999999998863 ) ;
#95132=ADVANCED_FACE ( 'NONE', ( #88462 ), #22439, .F. ) ;
#95133=DIRECTION ( 'NONE',  ( -0.000000000000000000, 0.3543493200069153248, 0.9351131265310292928 ) ) ;
#95135=LINE ( 'NONE', #72007, #124567 ) ;
#95138=ORIENTED_EDGE ( 'NONE', *, *, #35355, .T. ) ;
#95139=VECTOR ( 'NONE', #4535, 1000.000000000000000 ) ;
#95141=VECTOR ( 'NONE', #82739, 1000.000000000000114 ) ;
#95142=ORIENTED_EDGE ( 'NONE', *, *, #87454, .T. ) ;
#95143=AXIS2_PLACEMENT_3D ( 'NONE', #63028, #50697, #105754 ) ;
#95145=DIRECTION ( 'NONE',  ( -0.6830127018922180770, -0.6830127018922204085, -0.2588190451025213501 ) ) ;
#95146=VERTEX_POINT ( 'NONE', #78293 ) ;
#95147=VECTOR ( 'NONE', #132833, 1000.000000000000000 ) ;
#95148=ORIENTED_EDGE ( 'NONE', *, *, #98869, .T. ) ;
#95149=ORIENTED_EDGE ( 'NONE', *, *, #30596, .F. ) ;
#95150=LINE ( 'NONE', #93736, #97556 ) ;
#95151=ADVANCED_FACE ( 'NONE', ( #44993 ), #31221, .T. ) ;
#95152=DIRECTION ( 'NONE',  ( -1.000000000000000000, -3.109656758745491620E-14, 0.000000000000000000 ) ) ;
#95153=EDGE_LOOP ( 'NONE', ( #82473, #34643, #91713, #134392 ) ) ;
#95155=LINE ( 'NONE', #75566, #143553 ) ;
#95157=CARTESIAN_POINT ( 'NONE',  ( 11.99999999999992362, 13.55218569542903140, 5.000000000000000000 ) ) ;
#95160=VECTOR ( 'NONE', #50729, 1000.000000000000000 ) ;
#95161=CARTESIAN_POINT ( 'NONE',  ( 3.995075227788035477, -5.240707523384225297, 12.38332538355495238 ) ) ;
#95162=DIRECTION ( 'NONE',  ( 0.7071067811865486830, -0.7071067811865464625, -0.000000000000000000 ) ) ;
#95163=DIRECTION ( 'NONE',  ( -0.7071067811865486830, -0.7071067811865464625, -0.000000000000000000 ) ) ;
#95164=VERTEX_POINT ( 'NONE', #55114 ) ;
#95165=CARTESIAN_POINT ( 'NONE',  ( -27.15612307739222331, -22.22500000000000142, 4.000000000000000000 ) ) ;
#95166=ORIENTED_EDGE ( 'NONE', *, *, #6103, .F. ) ;
#95167=CARTESIAN_POINT ( 'NONE',  ( -18.18398860626898994, 28.73617430169800002, 5.000000000000000000 ) ) ;
#95168=CARTESIAN_POINT ( 'NONE',  ( 0.000000000000000000, 0.000000000000000000, 5.000000000000000000 ) ) ;
#95169=FACE_OUTER_BOUND ( 'NONE', #115997, .T. ) ;
#95170=EDGE_LOOP ( 'NONE', ( #72959, #72835, #35607, #48263 ) ) ;
#95172=VECTOR ( 'NONE', #70693, 1000.000000000000000 ) ;
#95174=DIRECTION ( 'NONE',  ( -0.3543493200069162685, -0.000000000000000000, -0.9351131265310288487 ) ) ;
#95175=CARTESIAN_POINT ( 'NONE',  ( -13.82816939922343380, 6.759292476615643253, 4.000000000000000000 ) ) ;
#95176=CARTESIAN_POINT ( 'NONE',  ( 9.792893218813395251, 0.7592924766157104211, 5.000000000000000000 ) ) ;
#95177=ORIENTED_EDGE ( 'NONE', *, *, #24278, .T. ) ;
#95178=LINE ( 'NONE', #85020, #120275 ) ;
#95179=LINE ( 'NONE', #18306, #128011 ) ;
#95181=DIRECTION ( 'NONE',  ( -0.7071067811865486830, -0.7071067811865464625, -0.000000000000000000 ) ) ;
#95182=DIRECTION ( 'NONE',  ( 0.7071067811865486830, -0.7071067811865464625, -0.000000000000000000 ) ) ;
#95183=ORIENTED_EDGE ( 'NONE', *, *, #18009, .T. ) ;
#95185=EDGE_CURVE ( 'NONE', #54925, #109538, #55839, .T. ) ;
#95188=FACE_OUTER_BOUND ( 'NONE', #96708, .T. ) ;
#95190=FACE_OUTER_BOUND ( 'NONE', #130731, .T. ) ;
#95191=EDGE_CURVE ( 'NONE', #58453, #99164, #19609, .T. ) ;
#95192=VECTOR ( 'NONE', #141101, 1000.000000000000000 ) ;
#95193=LINE ( 'NONE', #22601, #71484 ) ;
#95194=CARTESIAN_POINT ( 'NONE',  ( 34.49999999999976552, 3.653845994658424523, -4.504631822206450309 ) ) ;
#95195=EDGE_CURVE ( 'NONE', #9261, #99565, #86318, .T. ) ;
#95196=VERTEX_POINT ( 'NONE', #65293 ) ;
#95197=PLANE ( 'NONE',  #48857 ) ;
#95198=EDGE_CURVE ( 'NONE', #19553, #22039, #120312, .T. ) ;
#95199=DIRECTION ( 'NONE',  ( 0.7071067811865487940, 0.7071067811865463515, 0.000000000000000000 ) ) ;
#95200=VECTOR ( 'NONE', #43210, 1000.000000000000227 ) ;
#95201=DIRECTION ( 'NONE',  ( -0.000000000000000000, -0.3543493200069152693, 0.9351131265310292928 ) ) ;
#95202=VECTOR ( 'NONE', #18683, 1000.000000000000000 ) ;
#95204=EDGE_CURVE ( 'NONE', #49880, #99232, #64548, .T. ) ;
#95207=ORIENTED_EDGE ( 'NONE', *, *, #46108, .T. ) ;
#95208=CARTESIAN_POINT ( 'NONE',  ( -13.49999999999990408, 22.01701374228154506, 2.453858888625662704 ) ) ;
#95209=ORIENTED_EDGE ( 'NONE', *, *, #66473, .T. ) ;
#95210=EDGE_CURVE ( 'NONE', #114819, #43430, #52930, .T. ) ;
#95211=ORIENTED_EDGE ( 'NONE', *, *, #119713, .F. ) ;
#95213=DIRECTION ( 'NONE',  ( 0.7071067811865487940, 0.7071067811865463515, 0.000000000000000000 ) ) ;
#95214=PLANE ( 'NONE',  #143311 ) ;
#95215=CARTESIAN_POINT ( 'NONE',  ( -32.99999999999977973, -22.06887692260758982, 4.000000000000000000 ) ) ;
#95217=DIRECTION ( 'NONE',  ( -0.000000000000000000, 0.000000000000000000, 1.000000000000000000 ) ) ;
#95219=DIRECTION ( 'NONE',  ( -0.6830127018922181881, 0.6830127018922202975, -0.2588190451025214056 ) ) ;
#95220=ORIENTED_EDGE ( 'NONE', *, *, #88725, .T. ) ;
#95221=DIRECTION ( 'NONE',  ( 0.7071067811865486830, -0.7071067811865464625, -0.000000000000000000 ) ) ;
#95223=DIRECTION ( 'NONE',  ( -0.6830127018922181881, 0.6830127018922202975, -0.2588190451025214056 ) ) ;
#95224=AXIS2_PLACEMENT_3D ( 'NONE', #10181, #76177, #46440 ) ;
#95226=CARTESIAN_POINT ( 'NONE',  ( -5.483345613589513334, 22.22500000000000142, 4.500000000000000888 ) ) ;
#95227=EDGE_CURVE ( 'NONE', #68140, #62699, #76147, .T. ) ;
#95228=PLANE ( 'NONE',  #142965 ) ;
#95232=ORIENTED_EDGE ( 'NONE', *, *, #46483, .F. ) ;
#95234=CARTESIAN_POINT ( 'NONE',  ( -69.29974487139159578, -27.71228299555254537, 4.000000000000000000 ) ) ;
#95235=CARTESIAN_POINT ( 'NONE',  ( 57.29974487139158157, -27.71228299555246011, 4.000000000000000000 ) ) ;
#95237=ORIENTED_EDGE ( 'NONE', *, *, #37435, .T. ) ;
#95239=CARTESIAN_POINT ( 'NONE',  ( 45.29974487139158867, -27.71228299555237840, 4.000000000000000000 ) ) ;
#95240=VECTOR ( 'NONE', #52357, 1000.000000000000227 ) ;
#95241=VECTOR ( 'NONE', #34326, 1000.000000000000000 ) ;
#95244=ADVANCED_FACE ( 'NONE', ( #98595 ), #33392, .F. ) ;
#95245=CARTESIAN_POINT ( 'NONE',  ( 24.29974487139158867, -27.71228299555223273, 4.000000000000000000 ) ) ;
#95246=EDGE_LOOP ( 'NONE', ( #82183, #88298, #20080, #6027 ) ) ;
#95247=ORIENTED_EDGE ( 'NONE', *, *, #48479, .F. ) ;
#95248=VECTOR ( 'NONE', #45870, 1000.000000000000000 ) ;
#95249=AXIS2_PLACEMENT_3D ( 'NONE', #20851, #131781, #109301 ) ;
#95250=VECTOR ( 'NONE', #113629, 1000.000000000000000 ) ;
#95251=DIRECTION ( 'NONE',  ( -0.7071067811865486830, -0.7071067811865464625, 0.000000000000000000 ) ) ;
#95253=CARTESIAN_POINT ( 'NONE',  ( -14.99451991528749595, 28.92564299267948513, 4.000000000000000000 ) ) ;
#95254=CARTESIAN_POINT ( 'NONE',  ( 21.48921356237309155, -27.52281430457070499, 5.000000000000000000 ) ) ;
#95255=DIRECTION ( 'NONE',  ( 0.6830127018922181881, 0.6830127018922202975, -0.2588190451025214056 ) ) ;
#95256=DIRECTION ( 'NONE',  ( -0.3543493200069163240, 0.000000000000000000, 0.9351131265310288487 ) ) ;
#95257=FACE_OUTER_BOUND ( 'NONE', #79270, .T. ) ;
#95258=EDGE_LOOP ( 'NONE', ( #68785, #53092, #72428, #12369 ) ) ;
#95259=DIRECTION ( 'NONE',  ( 0.7071067811865486830, -0.7071067811865464625, -0.000000000000000000 ) ) ;
#95260=CARTESIAN_POINT ( 'NONE',  ( -29.47599861414530764, 22.03583458319437938, 4.979811245910090278 ) ) ;
#95261=CARTESIAN_POINT ( 'NONE',  ( -25.49999999999982236, -20.53675388469232743, 2.352720554255833818 ) ) ;
#95262=VECTOR ( 'NONE', #109705, 1000.000000000000227 ) ;
#95263=DIRECTION ( 'NONE',  ( 0.7071067811865486830, -0.7071067811865464625, -0.000000000000000000 ) ) ;
#95264=DIRECTION ( 'NONE',  ( -0.000000000000000000, -0.3543493200069152693, 0.9351131265310292928 ) ) ;
#95265=ORIENTED_EDGE ( 'NONE', *, *, #126139, .F. ) ;
#95266=EDGE_LOOP ( 'NONE', ( #50482, #23930, #32514, #36476 ) ) ;
#95267=AXIS2_PLACEMENT_3D ( 'NONE', #132255, #77165, #41634 ) ;
#95268=DIRECTION ( 'NONE',  ( -0.000000000000000000, 0.000000000000000000, 1.000000000000000000 ) ) ;
#95270=DIRECTION ( 'NONE',  ( -0.7071067811865486830, -0.7071067811865463515, 0.000000000000000000 ) ) ;
#95271=EDGE_CURVE ( 'NONE', #99346, #98689, #87731, .T. ) ;
#95274=ORIENTED_EDGE ( 'NONE', *, *, #132629, .F. ) ;
#95278=ORIENTED_EDGE ( 'NONE', *, *, #79973, .T. ) ;
#95279=VECTOR ( 'NONE', #21839, 999.9999999999998863 ) ;
#95280=VERTEX_POINT ( 'NONE', #135534 ) ;
#95281=VECTOR ( 'NONE', #34670, 999.9999999999998863 ) ;
#95282=ADVANCED_FACE ( 'NONE', ( #92709 ), #123238, .F. ) ;
#95283=DIRECTION ( 'NONE',  ( -0.7071067811865486830, -0.7071067811865464625, -0.000000000000000000 ) ) ;
#95284=VERTEX_POINT ( 'NONE', #103580 ) ;
#95285=VECTOR ( 'NONE', #88589, 1000.000000000000000 ) ;
#95287=VECTOR ( 'NONE', #20864, 1000.000000000000000 ) ;
#95288=EDGE_CURVE ( 'NONE', #109290, #7602, #125362, .T. ) ;
#95289=FACE_BOUND ( 'NONE', #131865, .T. ) ;
#95290=CARTESIAN_POINT ( 'NONE',  ( -17.24139925780192328, 21.72500000000000142, 5.000000000000000000 ) ) ;
#95291=CARTESIAN_POINT ( 'NONE',  ( -34.92500000000001137, -22.22500000000000142, 4.500000000000000888 ) ) ;
#95293=LINE ( 'NONE', #127202, #24897 ) ;
#95294=ORIENTED_EDGE ( 'NONE', *, *, #70403, .T. ) ;
#95295=DIRECTION ( 'NONE',  ( -0.6830127018922181881, 0.6830127018922202975, -0.2588190451025214056 ) ) ;
#95297=ORIENTED_EDGE ( 'NONE', *, *, #80612, .F. ) ;
#95298=EDGE_LOOP ( 'NONE', ( #120308, #55883, #59950, #84614 ) ) ;
#95300=ORIENTED_EDGE ( 'NONE', *, *, #140571, .F. ) ;
#95301=CARTESIAN_POINT ( 'NONE',  ( -22.99806943317885555, -22.22500000000000142, 4.500000000000000888 ) ) ;
#95302=CARTESIAN_POINT ( 'NONE',  ( -34.49999999999976552, 6.277155672890240012, -3.510561720658863738 ) ) ;
#95303=VECTOR ( 'NONE', #88863, 1000.000000000000000 ) ;
#95304=CARTESIAN_POINT ( 'NONE',  ( 33.18398860626899705, 28.73617430169810305, 5.000000000000000000 ) ) ;
#95305=VECTOR ( 'NONE', #74178, 1000.000000000000000 ) ;
#95306=CARTESIAN_POINT ( 'NONE',  ( -39.29974487139159578, -27.71228299555233576, 4.000000000000000000 ) ) ;
#95307=EDGE_LOOP ( 'NONE', ( #142767, #43156, #43763, #89236, #84593 ) ) ;
#95309=EDGE_CURVE ( 'NONE', #71472, #81871, #112345, .T. ) ;
#95310=LINE ( 'NONE', #81617, #59377 ) ;
#95311=LINE ( 'NONE', #81618, #126799 ) ;
#95312=AXIS2_PLACEMENT_3D ( 'NONE', #84645, #107092, #7767 ) ;
#95313=DIRECTION ( 'NONE',  ( 0.7071067811865487940, -0.7071067811865463515, 0.000000000000000000 ) ) ;
#95315=LINE ( 'NONE', #140262, #39307 ) ;
#95318=VERTEX_POINT ( 'NONE', #101451 ) ;
#95319=CARTESIAN_POINT ( 'NONE',  ( 9.850051285410186708, -8.240707523384193323, 17.25253755692241242 ) ) ;
#95320=( BOUNDED_CURVE ( )  B_SPLINE_CURVE ( 3, ( #123270, #66727, #89197, #12327 ),
 .UNSPECIFIED., .F., .T. ) 
 B_SPLINE_CURVE_WITH_KNOTS ( ( 4, 4 ),
 ( 5.005968288816719181, 5.074607125596323876 ),
 .UNSPECIFIED. ) 
 CURVE ( )  GEOMETRIC_REPRESENTATION_ITEM ( )  RATIONAL_B_SPLINE_CURVE ( ( 1.000000000000000000, 0.9996074310407765395, 0.9996074310407765395, 1.000000000000000000 ) ) 
 REPRESENTATION_ITEM ( '' )  );
#95321=LINE ( 'NONE', #117062, #58262 ) ;
#95322=ORIENTED_EDGE ( 'NONE', *, *, #122923, .F. ) ;
#95324=ORIENTED_EDGE ( 'NONE', *, *, #52904, .T. ) ;
#95326=VERTEX_POINT ( 'NONE', #124637 ) ;
#95328=AXIS2_PLACEMENT_3D ( 'NONE', #34452, #3231, #78676 ) ;
#95329=ORIENTED_EDGE ( 'NONE', *, *, #49623, .T. ) ;
#95331=ORIENTED_EDGE ( 'NONE', *, *, #139230, .T. ) ;
#95332=CARTESIAN_POINT ( 'NONE',  ( 33.48921356237309510, -27.52281430457078670, 5.000000000000000000 ) ) ;
#95333=ORIENTED_EDGE ( 'NONE', *, *, #14711, .F. ) ;
#95334=LINE ( 'NONE', #17075, #95040 ) ;
#95337=FACE_OUTER_BOUND ( 'NONE', #35394, .T. ) ;
#95338=ORIENTED_EDGE ( 'NONE', *, *, #26179, .T. ) ;
#95339=ORIENTED_EDGE ( 'NONE', *, *, #75145, .T. ) ;
#95340=EDGE_CURVE ( 'NONE', #92930, #123203, #58732, .T. ) ;
#95341=FACE_OUTER_BOUND ( 'NONE', #5962, .T. ) ;
#95342=VECTOR ( 'NONE', #137612, 1000.000000000000000 ) ;
#95344=ORIENTED_EDGE ( 'NONE', *, *, #66320, .F. ) ;
#95345=LINE ( 'NONE', #139609, #69007 ) ;
#95347=ORIENTED_EDGE ( 'NONE', *, *, #61253, .T. ) ;
#95349=ORIENTED_EDGE ( 'NONE', *, *, #85915, .T. ) ;
#95351=AXIS2_PLACEMENT_3D ( 'NONE', #109147, #43911, #21439 ) ;
#95352=AXIS2_PLACEMENT_3D ( 'NONE', #119977, #107698, #8357 ) ;
#95353=VECTOR ( 'NONE', #37684, 1000.000000000000000 ) ;
#95354=DIRECTION ( 'NONE',  ( 0.3543493200069162685, -0.000000000000000000, -0.9351131265310288487 ) ) ;
#95355=LINE ( 'NONE', #4719, #30944 ) ;
#95356=CARTESIAN_POINT ( 'NONE',  ( -51.48921356237309510, -27.52281430457091460, 5.000000000000000000 ) ) ;
#95357=VERTEX_POINT ( 'NONE', #69580 ) ;
#95359=EDGE_LOOP ( 'NONE', ( #1391, #65928, #109052, #97756 ) ) ;
#95360=PLANE ( 'NONE',  #72589 ) ;
#95362=CARTESIAN_POINT ( 'NONE',  ( 6.489213562373093325, -27.52281430457059841, 5.000000000000000000 ) ) ;
#95363=EDGE_CURVE ( 'NONE', #85586, #15513, #1400, .T. ) ;
#95364=ORIENTED_EDGE ( 'NONE', *, *, #11517, .T. ) ;
#95365=CARTESIAN_POINT ( 'NONE',  ( 23.48334561358938899, 22.22500000000000142, 4.500000000000000888 ) ) ;
#95366=DIRECTION ( 'NONE',  ( -0.7071067811865487940, 0.7071067811865463515, 0.000000000000000000 ) ) ;
#95368=EDGE_CURVE ( 'NONE', #32222, #22382, #3538, .T. ) ;
#95370=VERTEX_POINT ( 'NONE', #68861 ) ;
#95371=DIRECTION ( 'NONE',  ( 1.000000000000000000, 0.000000000000000000, 0.000000000000000000 ) ) ;
#95372=CARTESIAN_POINT ( 'NONE',  ( -23.54016161050245159, 18.75929247661552424, 8.305906642995433131 ) ) ;
#95374=DIRECTION ( 'NONE',  ( -0.7071067811865486830, 0.7071067811865464625, 0.000000000000000000 ) ) ;
#95375=LINE ( 'NONE', #139643, #38938 ) ;
#95378=EDGE_CURVE ( 'NONE', #79114, #130423, #90596, .T. ) ;
#95380=CARTESIAN_POINT ( 'NONE',  ( -5.999999999999956479, 15.45873954670184958, -0.03131636524292703144 ) ) ;
#95381=VECTOR ( 'NONE', #130965, 999.9999999999998863 ) ;
#95383=LINE ( 'NONE', #63514, #134445 ) ;
#95385=AXIS2_PLACEMENT_3D ( 'NONE', #20980, #98547, #35483 ) ;
#95386=CARTESIAN_POINT ( 'NONE',  ( 41.99451991528749062, 28.92564299267967343, 4.000000000000000000 ) ) ;
#95387=ORIENTED_EDGE ( 'NONE', *, *, #9920, .T. ) ;
#95389=VECTOR ( 'NONE', #65506, 1000.000000000000227 ) ;
#95391=DIRECTION ( 'NONE',  ( 0.7071067811865487940, -0.7071067811865463515, 0.000000000000000000 ) ) ;
#95392=LINE ( 'NONE', #139656, #111 ) ;
#95393=ORIENTED_EDGE ( 'NONE', *, *, #7475, .F. ) ;
#95394=EDGE_CURVE ( 'NONE', #106218, #131955, #102190, .T. ) ;
#95395=EDGE_CURVE ( 'NONE', #130550, #45511, #12299, .T. ) ;
#95396=CARTESIAN_POINT ( 'NONE',  ( 13.49999999999990408, -14.56887692260766443, 4.000000000000000000 ) ) ;
#95397=EDGE_LOOP ( 'NONE', ( #134816, #83721, #6868, #63745, #87678 ) ) ;
#95399=CARTESIAN_POINT ( 'NONE',  ( 15.18398860626900237, 28.73617430169797871, 5.000000000000000000 ) ) ;
#95400=LINE ( 'NONE', #6920, #67671 ) ;
#95402=CARTESIAN_POINT ( 'NONE',  ( 24.70710678118637205, -0.7407075233842718154, 5.000000000000000000 ) ) ;
#95403=EDGE_CURVE ( 'NONE', #104848, #52530, #15138, .T. ) ;
#95406=CARTESIAN_POINT ( 'NONE',  ( -14.99451991528749595, 28.92564299267948513, 4.000000000000000000 ) ) ;
#95407=ORIENTED_EDGE ( 'NONE', *, *, #29115, .F. ) ;
#95408=DIRECTION ( 'NONE',  ( 0.7071067811865487940, 0.7071067811865463515, 0.000000000000000000 ) ) ;
#95411=VECTOR ( 'NONE', #3424, 1000.000000000000227 ) ;
#95412=EDGE_CURVE ( 'NONE', #28959, #137771, #91324, .T. ) ;
#95413=CARTESIAN_POINT ( 'NONE',  ( 15.48921356237309510, -27.52281430457066236, 5.000000000000000000 ) ) ;
#95414=AXIS2_PLACEMENT_3D ( 'NONE', #16569, #37656, #15825 ) ;
#95415=ORIENTED_EDGE ( 'NONE', *, *, #102841, .F. ) ;
#95416=LINE ( 'NONE', #84566, #137063 ) ;
#95417=ORIENTED_EDGE ( 'NONE', *, *, #27579, .T. ) ;
#95419=LINE ( 'NONE', #140356, #15302 ) ;
#95420=EDGE_CURVE ( 'NONE', #106925, #102891, #56584, .T. ) ;
#95421=DIRECTION ( 'NONE',  ( 1.000000000000000000, 0.000000000000000000, 0.000000000000000000 ) ) ;
#95422=VECTOR ( 'NONE', #102171, 1000.000000000000000 ) ;
#95423=DIRECTION ( 'NONE',  ( 0.7071067811865487940, 0.7071067811865463515, 0.000000000000000000 ) ) ;
#95424=ORIENTED_EDGE ( 'NONE', *, *, #38607, .T. ) ;
#95425=CARTESIAN_POINT ( 'NONE',  ( 22.49999999999984368, 22.01701374228156638, 2.453858888625576995 ) ) ;
#95426=CARTESIAN_POINT ( 'NONE',  ( 15.79289321881334907, -2.240707523384260824, 5.000000000000000000 ) ) ;
#95427=DIRECTION ( 'NONE',  ( -0.6830127018922180770, -0.6830127018922204085, -0.2588190451025213501 ) ) ;
#95428=DIRECTION ( 'NONE',  ( -1.000000000000000000, 0.000000000000000000, 0.000000000000000000 ) ) ;
#95429=VERTEX_POINT ( 'NONE', #127493 ) ;
#95430=CARTESIAN_POINT ( 'NONE',  ( -3.183988606268992161, 28.73617430169789699, 5.000000000000000000 ) ) ;
#95432=VECTOR ( 'NONE', #108939, 999.9999999999998863 ) ;
#95436=EDGE_CURVE ( 'NONE', #126052, #17266, #94835, .T. ) ;
#95437=ORIENTED_EDGE ( 'NONE', *, *, #62455, .T. ) ;
#95439=ORIENTED_EDGE ( 'NONE', *, *, #68285, .F. ) ;
#95440=DIRECTION ( 'NONE',  ( 0.7071067811865486830, -0.7071067811865464625, -0.000000000000000000 ) ) ;
#95441=LINE ( 'NONE', #59984, #12986 ) ;
#95442=ORIENTED_EDGE ( 'NONE', *, *, #69011, .F. ) ;
#95443=VECTOR ( 'NONE', #86650, 1000.000000000000227 ) ;
#95444=AXIS2_PLACEMENT_3D ( 'NONE', #45747, #58794, #89919 ) ;
#95445=CARTESIAN_POINT ( 'NONE',  ( -3.516654386410431599, 22.22500000000000142, 4.500000000000000888 ) ) ;
#95446=CARTESIAN_POINT ( 'NONE',  ( -1.499999999999990896, 9.431123077392095766, 4.000000000000000000 ) ) ;
#95448=AXIS2_PLACEMENT_3D ( 'NONE', #35620, #124024, #24694 ) ;
#95450=ADVANCED_FACE ( 'NONE', ( #40505 ), #4950, .F. ) ;
#95452=CIRCLE ( 'NONE', #132552, 5.968999999999998529 ) ;
#95454=CARTESIAN_POINT ( 'NONE',  ( -34.92500000000001137, -22.22500000000000142, 4.000000000000000000 ) ) ;
#95455=VECTOR ( 'NONE', #72098, 1000.000000000000227 ) ;
#95459=EDGE_CURVE ( 'NONE', #115783, #44574, #93444, .T. ) ;
#95460=PLANE ( 'NONE',  #38561 ) ;
#95461=CARTESIAN_POINT ( 'NONE',  ( 36.48921356237310221, -27.52281430457080802, 5.000000000000000000 ) ) ;
#95462=LINE ( 'NONE', #49852, #118304 ) ;
#95463=LINE ( 'NONE', #116513, #130038 ) ;
#95464=DIRECTION ( 'NONE',  ( -0.000000000000000000, 0.3543493200069153248, 0.9351131265310292928 ) ) ;
#95466=ORIENTED_EDGE ( 'NONE', *, *, #95412, .T. ) ;
#95469=EDGE_CURVE ( 'NONE', #132519, #85530, #139099, .T. ) ;
#95473=ORIENTED_EDGE ( 'NONE', *, *, #116679, .T. ) ;
#95474=DIRECTION ( 'NONE',  ( -0.000000000000000000, -0.3543493200069152693, 0.9351131265310292928 ) ) ;
#95475=ADVANCED_FACE ( 'NONE', ( #26750 ), #84028, .F. ) ;
#95477=DIRECTION ( 'NONE',  ( -0.7071067811865486830, 0.7071067811865464625, 0.000000000000000000 ) ) ;
#95478=LINE ( 'NONE', #73060, #104029 ) ;
#95479=VECTOR ( 'NONE', #109344, 1000.000000000000227 ) ;
#95480=CARTESIAN_POINT ( 'NONE',  ( 29.99999999999979039, -8.731860332648819778, -2.120594902707469309 ) ) ;
#95482=CARTESIAN_POINT ( 'NONE',  ( -32.99999999999976552, -9.033600742197641864, 5.000000000000000000 ) ) ;
#95484=ORIENTED_EDGE ( 'NONE', *, *, #121653, .T. ) ;
#95485=EDGE_CURVE ( 'NONE', #115809, #51152, #84705, .T. ) ;
#95486=LINE ( 'NONE', #83946, #50381 ) ;
#95489=EDGE_CURVE ( 'NONE', #12889, #51279, #83281, .T. ) ;
#95492=VERTEX_POINT ( 'NONE', #38352 ) ;
#95493=CARTESIAN_POINT ( 'NONE',  ( 0.000000000000000000, 0.000000000000000000, 5.000000000000000000 ) ) ;
#95494=DIRECTION ( 'NONE',  ( 0.000000000000000000, 0.000000000000000000, 1.000000000000000000 ) ) ;
#95496=FACE_OUTER_BOUND ( 'NONE', #94302, .T. ) ;
#95497=EDGE_CURVE ( 'NONE', #100985, #139718, #128224, .T. ) ;
#95498=VECTOR ( 'NONE', #120764, 999.9999999999998863 ) ;
#95499=CARTESIAN_POINT ( 'NONE',  ( -2.816011393730999401, 28.73617430169785436, 5.000000000000000000 ) ) ;
#95500=DIRECTION ( 'NONE',  ( -0.6830127018922181881, 0.6830127018922202975, -0.2588190451025214056 ) ) ;
#95501=CARTESIAN_POINT ( 'NONE',  ( -12.79333936457838661, 21.75929247661549581, 4.998822639870701856 ) ) ;
#95502=VECTOR ( 'NONE', #130204, 1000.000000000000000 ) ;
#95504=ADVANCED_FACE ( 'NONE', ( #28188 ), #73828, .F. ) ;
#95505=FACE_OUTER_BOUND ( 'NONE', #124431, .T. ) ;
#95507=ORIENTED_EDGE ( 'NONE', *, *, #14169, .T. ) ;
#95508=DIRECTION ( 'NONE',  ( -0.7071067811865486830, -0.7071067811865464625, 0.000000000000000000 ) ) ;
#95509=LINE ( 'NONE', #139773, #28970 ) ;
#95510=ORIENTED_EDGE ( 'NONE', *, *, #128991, .T. ) ;
#95511=VERTEX_POINT ( 'NONE', #5687 ) ;
#95512=ORIENTED_EDGE ( 'NONE', *, *, #104573, .T. ) ;
#95515=CARTESIAN_POINT ( 'NONE',  ( 42.18398860626899705, 28.73617430169816700, 5.000000000000000000 ) ) ;
#95516=FACE_OUTER_BOUND ( 'NONE', #131287, .T. ) ;
#95517=LINE ( 'NONE', #7048, #92642 ) ;
#95518=CARTESIAN_POINT ( 'NONE',  ( -23.99999999999983302, -12.03360074219761344, 5.000000000000000000 ) ) ;
#95519=ORIENTED_EDGE ( 'NONE', *, *, #60355, .T. ) ;
#95521=VECTOR ( 'NONE', #13196, 1000.000000000000000 ) ;
#95522=ORIENTED_EDGE ( 'NONE', *, *, #35829, .T. ) ;
#95524=PLANE ( 'NONE',  #63220 ) ;
#95525=ADVANCED_FACE ( 'NONE', ( #52080 ), #95571, .F. ) ;
#95526=LINE ( 'NONE', #26714, #32040 ) ;
#95528=ORIENTED_EDGE ( 'NONE', *, *, #627, .F. ) ;
#95529=EDGE_CURVE ( 'NONE', #14760, #65516, #60120, .T. ) ;
#95530=ORIENTED_EDGE ( 'NONE', *, *, #47581, .F. ) ;
#95531=ORIENTED_EDGE ( 'NONE', *, *, #22332, .T. ) ;
#95532=CARTESIAN_POINT ( 'NONE',  ( -8.207106781186482181, -8.240707523384203981, 5.000000000000000000 ) ) ;
#95535=CARTESIAN_POINT ( 'NONE',  ( -23.99451991528749062, 28.92564299267954908, 4.000000000000000000 ) ) ;
#95536=VECTOR ( 'NONE', #56108, 1000.000000000000000 ) ;
#95537=DIRECTION ( 'NONE',  ( -0.7071067811865486830, -0.7071067811865464625, 0.000000000000000000 ) ) ;
#95538=CARTESIAN_POINT ( 'NONE',  ( 0.000000000000000000, 0.000000000000000000, 5.000000000000000000 ) ) ;
#95539=EDGE_CURVE ( 'NONE', #140292, #107648, #82568, .T. ) ;
#95540=AXIS2_PLACEMENT_3D ( 'NONE', #135673, #48662, #115286 ) ;
#95541=EDGE_CURVE ( 'NONE', #4615, #119637, #138092, .T. ) ;
#95542=DIRECTION ( 'NONE',  ( -0.000000000000000000, 0.3543493200069153248, 0.9351131265310292928 ) ) ;
#95543=CARTESIAN_POINT ( 'NONE',  ( 10.49999999999993072, 12.05218569542904561, 5.000000000000000000 ) ) ;
#95544=VECTOR ( 'NONE', #132269, 1000.000000000000000 ) ;
#95545=FACE_OUTER_BOUND ( 'NONE', #55519, .T. ) ;
#95546=CARTESIAN_POINT ( 'NONE',  ( 51.48921356237309510, -27.52281430457091460, 5.000000000000000000 ) ) ;
#95547=VERTEX_POINT ( 'NONE', #104286 ) ;
#95548=CARTESIAN_POINT ( 'NONE',  ( -19.49999999999987210, 10.08746187583915344, 4.000000000000000000 ) ) ;
#95552=DIRECTION ( 'NONE',  ( 0.7071067811865487940, 0.7071067811865463515, 0.000000000000000000 ) ) ;
#95553=EDGE_CURVE ( 'NONE', #47748, #69243, #105709, .T. ) ;
#95554=ORIENTED_EDGE ( 'NONE', *, *, #26202, .F. ) ;
#95555=CARTESIAN_POINT ( 'NONE',  ( 15.00548008471250228, 28.92564299267927552, 4.000000000000000000 ) ) ;
#95556=CARTESIAN_POINT ( 'NONE',  ( -2.207106781186521260, -14.24070752338414003, 5.000000000000000000 ) ) ;
#95557=EDGE_LOOP ( 'NONE', ( #28935, #119398, #48010, #130225 ) ) ;
#95558=EDGE_CURVE ( 'NONE', #23935, #90194, #15824, .T. ) ;
#95559=EDGE_CURVE ( 'NONE', #123136, #48695, #50646, .T. ) ;
#95560=LINE ( 'NONE', #71692, #100114 ) ;
#95562=ORIENTED_EDGE ( 'NONE', *, *, #30578, .F. ) ;
#95563=PLANE ( 'NONE',  #127661 ) ;
#95564=ORIENTED_EDGE ( 'NONE', *, *, #50693, .F. ) ;
#95565=CARTESIAN_POINT ( 'NONE',  ( 34.92499999999998295, 12.31448516125888126, 8.755464546898146239 ) ) ;
#95568=CARTESIAN_POINT ( 'NONE',  ( 0.000000000000000000, 0.000000000000000000, 5.000000000000000000 ) ) ;
#95570=ADVANCED_FACE ( 'NONE', ( #110011 ), #31756, .T. ) ;
#95571=PLANE ( 'NONE',  #115642 ) ;
#95572=CARTESIAN_POINT ( 'NONE',  ( -31.17183060077625356, 18.75929247661552068, 4.000000000000000000 ) ) ;
#95573=LINE ( 'NONE', #17979, #17038 ) ;
#95574=LINE ( 'NONE', #117308, #94672 ) ;
#95577=EDGE_CURVE ( 'NONE', #74437, #35117, #54950, .T. ) ;
#95578=DIRECTION ( 'NONE',  ( -0.7071067811865486830, 0.7071067811865464625, 0.000000000000000000 ) ) ;
#95579=CARTESIAN_POINT ( 'NONE',  ( 12.79289321881336683, 9.759292476615623713, 5.000000000000000000 ) ) ;
#95580=VERTEX_POINT ( 'NONE', #142657 ) ;
#95581=VECTOR ( 'NONE', #17915, 1000.000000000000227 ) ;
#95582=ORIENTED_EDGE ( 'NONE', *, *, #54175, .T. ) ;
#95585=VERTEX_POINT ( 'NONE', #33223 ) ;
#95588=DIRECTION ( 'NONE',  ( -0.6830127018922180770, -0.6830127018922204085, -0.2588190451025213501 ) ) ;
#95589=EDGE_CURVE ( 'NONE', #119974, #118230, #121598, .T. ) ;
#95590=PLANE ( 'NONE',  #1601 ) ;
#95591=ORIENTED_EDGE ( 'NONE', *, *, #121114, .T. ) ;
#95593=DIRECTION ( 'NONE',  ( -0.7071067811865486830, -0.7071067811865464625, 0.000000000000000000 ) ) ;
#95594=CARTESIAN_POINT ( 'NONE',  ( 25.49999999999982947, -5.568876922607755908, 4.000000000000000000 ) ) ;
#95595=CARTESIAN_POINT ( 'NONE',  ( 0.000000000000000000, 0.000000000000000000, 5.000000000000000000 ) ) ;
#95596=CARTESIAN_POINT ( 'NONE',  ( -20.99999999999985434, -11.35517001088073563, -1.126524801160159406 ) ) ;
#95597=EDGE_LOOP ( 'NONE', ( #52819, #110191, #120946, #108058 ) ) ;
#95598=DIRECTION ( 'NONE',  ( -0.000000000000000000, 0.000000000000000000, 1.000000000000000000 ) ) ;
#95599=EDGE_CURVE ( 'NONE', #101632, #71694, #141968, .T. ) ;
#95600=LINE ( 'NONE', #83318, #59213 ) ;
#95601=DIRECTION ( 'NONE',  ( 0.7071067811865487940, -0.7071067811865463515, 0.000000000000000000 ) ) ;
#95602=PLANE ( 'NONE',  #126246 ) ;
#95603=CARTESIAN_POINT ( 'NONE',  ( 27.48921356237309155, -27.52281430457074762, 5.000000000000000000 ) ) ;
#95605=VECTOR ( 'NONE', #93432, 999.9999999999998863 ) ;
#95606=EDGE_CURVE ( 'NONE', #108986, #134910, #52767, .T. ) ;
#95607=VERTEX_POINT ( 'NONE', #77434 ) ;
#95608=ORIENTED_EDGE ( 'NONE', *, *, #114565, .T. ) ;
#95610=VERTEX_POINT ( 'NONE', #21595 ) ;
#95611=VECTOR ( 'NONE', #80187, 999.9999999999998863 ) ;
#95613=VECTOR ( 'NONE', #29266, 999.9999999999998863 ) ;
#95614=DIRECTION ( 'NONE',  ( -0.7071067811865486830, -0.7071067811865464625, 0.000000000000000000 ) ) ;
#95616=EDGE_CURVE ( 'NONE', #78422, #42250, #65856, .T. ) ;
#95617=DIRECTION ( 'NONE',  ( 0.3543493200069162685, -0.000000000000000000, -0.9351131265310288487 ) ) ;
#95618=CARTESIAN_POINT ( 'NONE',  ( 10.49999999999992539, -10.04351517176477593, -1.623559851933798814 ) ) ;
#95620=ORIENTED_EDGE ( 'NONE', *, *, #47870, .F. ) ;
#95621=DIRECTION ( 'NONE',  ( 0.000000000000000000, 1.000000000000000000, 0.000000000000000000 ) ) ;
#95623=CARTESIAN_POINT ( 'NONE',  ( -30.29974487139158867, -27.71228299555227537, 4.000000000000000000 ) ) ;
#95624=AXIS2_PLACEMENT_3D ( 'NONE', #72884, #6094, #50371 ) ;
#95625=CARTESIAN_POINT ( 'NONE',  ( 2.994519915287485734, 28.92564299267940342, 4.000000000000000000 ) ) ;
#95626=CARTESIAN_POINT ( 'NONE',  ( 34.92499999999998295, 10.70193056682087906, 4.500000000000000888 ) ) ;
#95627=ORIENTED_EDGE ( 'NONE', *, *, #54998, .F. ) ;
#95628=VERTEX_POINT ( 'NONE', #20139 ) ;
#95631=LINE ( 'NONE', #139887, #70867 ) ;
#95633=VECTOR ( 'NONE', #18738, 999.9999999999998863 ) ;
#95636=EDGE_LOOP ( 'NONE', ( #56734, #135503, #60674, #9733, #143494 ) ) ;
#95639=EDGE_CURVE ( 'NONE', #34606, #93313, #88287, .T. ) ;
#95640=VERTEX_POINT ( 'NONE', #75973 ) ;
#95641=AXIS2_PLACEMENT_3D ( 'NONE', #142120, #23131, #20292 ) ;
#95643=CARTESIAN_POINT ( 'NONE',  ( -18.18398860626898994, 28.73617430169800002, 5.000000000000000000 ) ) ;
#95644=ORIENTED_EDGE ( 'NONE', *, *, #136762, .T. ) ;
#95645=DIRECTION ( 'NONE',  ( -0.3543493200069162685, -0.000000000000000000, -0.9351131265310288487 ) ) ;
#95646=CARTESIAN_POINT ( 'NONE',  ( -17.29387692260792520, 22.22500000000000142, 4.000000000000000000 ) ) ;
#95647=AXIS2_PLACEMENT_3D ( 'NONE', #49498, #129149, #7353 ) ;
#95649=CARTESIAN_POINT ( 'NONE',  ( 3.299744871391591339, -27.71228299555208352, 4.000000000000000000 ) ) ;
#95650=CARTESIAN_POINT ( 'NONE',  ( 39.48921356237310221, -27.52281430457082934, 5.000000000000000000 ) ) ;
#95651=ORIENTED_EDGE ( 'NONE', *, *, #42775, .T. ) ;
#95652=DIRECTION ( 'NONE',  ( -0.7071067811865486830, -0.7071067811865464625, 0.000000000000000000 ) ) ;
#95654=ORIENTED_EDGE ( 'NONE', *, *, #132508, .F. ) ;
#95655=LINE ( 'NONE', #6461, #71267 ) ;
#95656=EDGE_CURVE ( 'NONE', #54552, #109346, #99115, .T. ) ;
#95658=CARTESIAN_POINT ( 'NONE',  ( 5.510786437626906675, -27.52281430457051314, 5.000000000000000000 ) ) ;
#95659=ORIENTED_EDGE ( 'NONE', *, *, #44549, .F. ) ;
#95660=CARTESIAN_POINT ( 'NONE',  ( 15.07843108771893981, 22.22500000000000142, 23.94816926554818082 ) ) ;
#95661=EDGE_CURVE ( 'NONE', #66820, #57955, #120144, .T. ) ;
#95662=ORIENTED_EDGE ( 'NONE', *, *, #108438, .F. ) ;
#95663=ORIENTED_EDGE ( 'NONE', *, *, #7194, .T. ) ;
#95664=ORIENTED_EDGE ( 'NONE', *, *, #35700, .T. ) ;
#95666=EDGE_CURVE ( 'NONE', #45614, #25745, #109307, .T. ) ;
#95668=VECTOR ( 'NONE', #3021, 1000.000000000000227 ) ;
#95669=CARTESIAN_POINT ( 'NONE',  ( -23.99999999999983302, -18.41253812416056945, 4.000000000000000000 ) ) ;
#95670=CARTESIAN_POINT ( 'NONE',  ( 66.48921356237309510, -27.52281430457101763, 5.000000000000000000 ) ) ;
#95673=EDGE_CURVE ( 'NONE', #12211, #3321, #74559, .T. ) ;
#95674=FACE_OUTER_BOUND ( 'NONE', #94609, .T. ) ;
#95675=DIRECTION ( 'NONE',  ( -0.000000000000000000, -0.3543493200069152693, 0.9351131265310292928 ) ) ;
#95676=VECTOR ( 'NONE', #117770, 1000.000000000000000 ) ;
#95677=CARTESIAN_POINT ( 'NONE',  ( -15.79289321881334551, -14.24070752338414358, 5.000000000000000000 ) ) ;
#95678=EDGE_CURVE ( 'NONE', #49326, #56431, #9991, .T. ) ;
#95679=CARTESIAN_POINT ( 'NONE',  ( -28.63753812416077693, 22.22499999999999432, 4.000000000000000000 ) ) ;
#95681=LINE ( 'NONE', #139937, #54103 ) ;
#95682=ORIENTED_EDGE ( 'NONE', *, *, #135034, .T. ) ;
#95684=ORIENTED_EDGE ( 'NONE', *, *, #89518, .F. ) ;
#95685=ORIENTED_EDGE ( 'NONE', *, *, #135474, .F. ) ;
#95686=VERTEX_POINT ( 'NONE', #31058 ) ;
#95687=CARTESIAN_POINT ( 'NONE',  ( 17.99451991528748351, 28.92564299267950645, 4.000000000000000000 ) ) ;
#95689=ORIENTED_EDGE ( 'NONE', *, *, #84623, .F. ) ;
#95693=LINE ( 'NONE', #119560, #6368 ) ;
#95694=LINE ( 'NONE', #71837, #17776 ) ;
#95695=PLANE ( 'NONE',  #71789 ) ;
#95696=VERTEX_POINT ( 'NONE', #134658 ) ;
#95697=CARTESIAN_POINT ( 'NONE',  ( -2.671830600776449405, -9.740707523384187994, 4.000000000000000000 ) ) ;
#95698=EDGE_CURVE ( 'NONE', #140787, #79481, #72506, .T. ) ;
#95699=VERTEX_POINT ( 'NONE', #79598 ) ;
#95700=CARTESIAN_POINT ( 'NONE',  ( -30.29974487139158867, -27.71228299555227537, 4.000000000000000000 ) ) ;
#95701=AXIS2_PLACEMENT_3D ( 'NONE', #19183, #51830, #31493 ) ;
#95702=LINE ( 'NONE', #142783, #42752 ) ;
#95703=VECTOR ( 'NONE', #38150, 1000.000000000000000 ) ;
#95705=EDGE_LOOP ( 'NONE', ( #38128, #139303, #115649, #93457 ) ) ;
#95709=CARTESIAN_POINT ( 'NONE',  ( -42.18398860626899705, 28.73617430169816700, 5.000000000000000000 ) ) ;
#95711=ADVANCED_FACE ( 'NONE', ( #123782 ), #90411, .F. ) ;
#95712=EDGE_LOOP ( 'NONE', ( #119503, #41114, #46611 ) ) ;
#95713=CARTESIAN_POINT ( 'NONE',  ( -7.499999999999944045, -14.56887692260766087, 4.000000000000000000 ) ) ;
#95714=ORIENTED_EDGE ( 'NONE', *, *, #51129, .T. ) ;
#95717=DIRECTION ( 'NONE',  ( 0.6830127018922181881, 0.6830127018922202975, -0.2588190451025214056 ) ) ;
#95718=CARTESIAN_POINT ( 'NONE',  ( 0.000000000000000000, 7.931123077392108200, 4.000000000000000000 ) ) ;
#95720=( BOUNDED_CURVE ( )  B_SPLINE_CURVE ( 3, ( #114391, #15061, #126678, #59339 ),
 .UNSPECIFIED., .F., .F. ) 
 B_SPLINE_CURVE_WITH_KNOTS ( ( 4, 4 ),
 ( 1.901594255663637600, 1.933014472006564954 ),
 .UNSPECIFIED. ) 
 CURVE ( )  GEOMETRIC_REPRESENTATION_ITEM ( )  RATIONAL_B_SPLINE_CURVE ( ( 1.000000000000000000, 0.9999177325257868620, 0.9999177325257868620, 1.000000000000000000 ) ) 
 REPRESENTATION_ITEM ( '' )  );
#95722=ADVANCED_FACE ( 'NONE', ( #100592 ), #123053, .F. ) ;
#95723=EDGE_CURVE ( 'NONE', #123801, #126581, #12830, .T. ) ;
#95725=FACE_OUTER_BOUND ( 'NONE', #81020, .T. ) ;
#95726=CARTESIAN_POINT ( 'NONE',  ( -45.18398860626900415, 28.73617430169818832, 5.000000000000000000 ) ) ;
#95727=ORIENTED_EDGE ( 'NONE', *, *, #27445, .F. ) ;
#95728=LINE ( 'NONE', #120295, #86014 ) ;
#95729=VECTOR ( 'NONE', #54728, 1000.000000000000000 ) ;
#95730=DIRECTION ( 'NONE',  ( -0.7071067811865487940, 0.7071067811865463515, 0.000000000000000000 ) ) ;
#95731=EDGE_CURVE ( 'NONE', #123966, #41451, #1233, .T. ) ;
#95732=EDGE_LOOP ( 'NONE', ( #80947, #72107, #135133, #41516 ) ) ;
#95733=CARTESIAN_POINT ( 'NONE',  ( 32.99999999999975842, 17.58746187583907528, 4.000000000000000000 ) ) ;
#95734=EDGE_LOOP ( 'NONE', ( #24762, #137171, #32709, #88225 ) ) ;
#95735=EDGE_CURVE ( 'NONE', #13057, #49717, #114303, .T. ) ;
#95736=VECTOR ( 'NONE', #125038, 1000.000000000000000 ) ;
#95737=CARTESIAN_POINT ( 'NONE',  ( 63.18398860626900415, 28.73617430169831621, 5.000000000000000000 ) ) ;
#95738=PLANE ( 'NONE',  #41463 ) ;
#95740=DIRECTION ( 'NONE',  ( -0.6830127018922180770, -0.6830127018922204085, -0.2588190451025213501 ) ) ;
#95741=LINE ( 'NONE', #118917, #42930 ) ;
#95742=LINE ( 'NONE', #71164, #80813 ) ;
#95744=EDGE_CURVE ( 'NONE', #63240, #21420, #91156, .T. ) ;
#95745=LINE ( 'NONE', #40668, #113291 ) ;
#95746=LINE ( 'NONE', #5132, #268 ) ;
#95747=FACE_OUTER_BOUND ( 'NONE', #58701, .T. ) ;
#95748=LINE ( 'NONE', #127685, #84233 ) ;
#95749=CARTESIAN_POINT ( 'NONE',  ( -18.48921356237309510, -27.52281430457068367, 5.000000000000000000 ) ) ;
#95753=DIRECTION ( 'NONE',  ( -0.000000000000000000, 0.000000000000000000, 1.000000000000000000 ) ) ;
#95754=DIRECTION ( 'NONE',  ( 0.7071067811865487940, -0.7071067811865463515, 0.000000000000000000 ) ) ;
#95755=ORIENTED_EDGE ( 'NONE', *, *, #27646, .T. ) ;
#95756=VECTOR ( 'NONE', #30225, 1000.000000000000227 ) ;
#95757=ORIENTED_EDGE ( 'NONE', *, *, #50390, .F. ) ;
#95758=ORIENTED_EDGE ( 'NONE', *, *, #82878, .T. ) ;
#95760=VERTEX_POINT ( 'NONE', #112874 ) ;
#95761=ORIENTED_EDGE ( 'NONE', *, *, #116712, .F. ) ;
#95762=ORIENTED_EDGE ( 'NONE', *, *, #70203, .T. ) ;
#95763=DIRECTION ( 'NONE',  ( -0.7071067811865486830, -0.7071067811865464625, 0.000000000000000000 ) ) ;
#95766=CARTESIAN_POINT ( 'NONE',  ( -34.42500000000001137, 0.000000000000000000, 4.500000000000000888 ) ) ;
#95767=DIRECTION ( 'NONE',  ( -0.6830127018922181881, 0.6830127018922202975, -0.2588190451025214056 ) ) ;
#95769=CARTESIAN_POINT ( 'NONE',  ( 5.292893218813423672, -15.74070752338412049, 5.000000000000000000 ) ) ;
#95771=ORIENTED_EDGE ( 'NONE', *, *, #103230, .F. ) ;
#95773=LINE ( 'NONE', #116812, #70162 ) ;
#95774=LINE ( 'NONE', #129836, #56709 ) ;
#95776=VECTOR ( 'NONE', #140759, 1000.000000000000000 ) ;
#95777=PLANE ( 'NONE',  #139556 ) ;
#95778=CARTESIAN_POINT ( 'NONE',  ( -75.48921356237309510, -27.52281430457107803, 5.000000000000000000 ) ) ;
#95780=PLANE ( 'NONE',  #49055 ) ;
#95781=EDGE_CURVE ( 'NONE', #119711, #48518, #58561, .T. ) ;
#95782=VECTOR ( 'NONE', #21766, 1000.000000000000000 ) ;
#95783=DIRECTION ( 'NONE',  ( -0.7071067811865486830, -0.7071067811865464625, -0.000000000000000000 ) ) ;
#95784=ORIENTED_EDGE ( 'NONE', *, *, #137776, .F. ) ;
#95785=ORIENTED_EDGE ( 'NONE', *, *, #44495, .F. ) ;
#95788=DIRECTION ( 'NONE',  ( -0.000000000000000000, -1.000000000000000000, -0.000000000000000000 ) ) ;
#95789=CARTESIAN_POINT ( 'NONE',  ( 57.29974487139158157, -27.71228299555246011, 4.000000000000000000 ) ) ;
#95791=VECTOR ( 'NONE', #22571, 1000.000000000000000 ) ;
#95792=DIRECTION ( 'NONE',  ( -0.7071067811865486830, -0.7071067811865464625, -0.000000000000000000 ) ) ;
#95793=DIRECTION ( 'NONE',  ( -0.7071067811865487940, 0.7071067811865463515, 0.000000000000000000 ) ) ;
#95796=VECTOR ( 'NONE', #36361, 1000.000000000000000 ) ;
#95797=ORIENTED_EDGE ( 'NONE', *, *, #9807, .T. ) ;
#95798=AXIS2_PLACEMENT_3D ( 'NONE', #19824, #32893, #44487 ) ;
#95800=ORIENTED_EDGE ( 'NONE', *, *, #63667, .T. ) ;
#95801=DIRECTION ( 'NONE',  ( 0.3543493200069162685, -0.000000000000000000, -0.9351131265310288487 ) ) ;
#95804=DIRECTION ( 'NONE',  ( -0.6830127018922181881, 0.6830127018922202975, -0.2588190451025214056 ) ) ;
#95805=ORIENTED_EDGE ( 'NONE', *, *, #89615, .T. ) ;
#95807=ORIENTED_EDGE ( 'NONE', *, *, #80021, .T. ) ;
#95808=DIRECTION ( 'NONE',  ( -0.7071067811865486830, -0.7071067811865464625, -0.000000000000000000 ) ) ;
#95809=CARTESIAN_POINT ( 'NONE',  ( 27.48921356237309155, -27.52281430457074762, 5.000000000000000000 ) ) ;
#95810=FACE_OUTER_BOUND ( 'NONE', #129307, .T. ) ;
#95811=DIRECTION ( 'NONE',  ( 0.7071067811865487940, 0.7071067811865463515, -0.000000000000000000 ) ) ;
#95812=AXIS2_PLACEMENT_3D ( 'NONE', #83092, #49777, #49049 ) ;
#95813=AXIS2_PLACEMENT_3D ( 'NONE', #24188, #101014, #1667 ) ;
#95816=ORIENTED_EDGE ( 'NONE', *, *, #108294, .T. ) ;
#95817=LINE ( 'NONE', #140065, #24702 ) ;
#95818=ORIENTED_EDGE ( 'NONE', *, *, #56575, .T. ) ;
#95819=EDGE_LOOP ( 'NONE', ( #126405, #133027, #68735, #16907 ) ) ;
#95821=ORIENTED_EDGE ( 'NONE', *, *, #53395, .T. ) ;
#95823=ORIENTED_EDGE ( 'NONE', *, *, #5703, .F. ) ;
#95824=EDGE_CURVE ( 'NONE', #85885, #106040, #122301, .T. ) ;
#95825=EDGE_CURVE ( 'NONE', #41816, #36553, #13537, .T. ) ;
#95826=PLANE ( 'NONE',  #61845 ) ;
#95827=AXIS2_PLACEMENT_3D ( 'NONE', #65985, #22411, #11528 ) ;
#95828=DIRECTION ( 'NONE',  ( -0.000000000000000000, 0.000000000000000000, 1.000000000000000000 ) ) ;
#95829=EDGE_CURVE ( 'NONE', #16704, #64740, #12123, .T. ) ;
#95830=FACE_BOUND ( 'NONE', #85765, .T. ) ;
#95831=DIRECTION ( 'NONE',  ( 0.7071067811865487940, 0.7071067811865463515, 0.000000000000000000 ) ) ;
#95833=EDGE_CURVE ( 'NONE', #9322, #73005, #33908, .T. ) ;
#95835=CARTESIAN_POINT ( 'NONE',  ( -19.17183060077633172, 15.75929247661555976, 4.000000000000000000 ) ) ;
#95836=EDGE_LOOP ( 'NONE', ( #142875, #101400, #70733, #20746 ) ) ;
#95838=ORIENTED_EDGE ( 'NONE', *, *, #14467, .T. ) ;
#95840=DIRECTION ( 'NONE',  ( 0.3543493200069162685, -0.000000000000000000, -0.9351131265310288487 ) ) ;
#95842=ADVANCED_FACE ( 'NONE', ( #17142 ), #72992, .F. ) ;
#95845=VECTOR ( 'NONE', #99238, 1000.000000000000000 ) ;
#95846=ORIENTED_EDGE ( 'NONE', *, *, #74222, .F. ) ;
#95847=CARTESIAN_POINT ( 'NONE',  ( -17.81601139373099940, 28.73617430169775133, 5.000000000000000000 ) ) ;
#95848=PLANE ( 'NONE',  #14828 ) ;
#95850=ORIENTED_EDGE ( 'NONE', *, *, #96843, .T. ) ;
#95851=CARTESIAN_POINT ( 'NONE',  ( -34.92500000000001137, -22.22500000000000142, 4.500000000000000888 ) ) ;
#95853=EDGE_CURVE ( 'NONE', #17670, #136430, #17822, .T. ) ;
#95855=DIRECTION ( 'NONE',  ( -0.6830127018922180770, -0.6830127018922204085, -0.2588190451025213501 ) ) ;
#95856=LINE ( 'NONE', #40783, #20337 ) ;
#95857=DIRECTION ( 'NONE',  ( -0.3543493200069162685, -0.000000000000000000, -0.9351131265310288487 ) ) ;
#95859=ORIENTED_EDGE ( 'NONE', *, *, #112509, .F. ) ;
#95860=VERTEX_POINT ( 'NONE', #62095 ) ;
#95861=CARTESIAN_POINT ( 'NONE',  ( 31.49999999999977973, -1.533600742197722910, 5.000000000000000000 ) ) ;
#95862=FACE_OUTER_BOUND ( 'NONE', #87816, .T. ) ;
#95863=ORIENTED_EDGE ( 'NONE', *, *, #20260, .F. ) ;
#95865=VERTEX_POINT ( 'NONE', #125915 ) ;
#95866=FACE_OUTER_BOUND ( 'NONE', #12454, .T. ) ;
#95867=LINE ( 'NONE', #120436, #69305 ) ;
#95868=ORIENTED_EDGE ( 'NONE', *, *, #131598, .F. ) ;
#95869=LINE ( 'NONE', #18281, #97250 ) ;
#95872=PLANE ( 'NONE',  #84009 ) ;
#95873=VECTOR ( 'NONE', #96617, 1000.000000000000000 ) ;
#95875=LINE ( 'NONE', #78252, #119022 ) ;
#95876=VERTEX_POINT ( 'NONE', #128066 ) ;
#95879=PLANE ( 'NONE',  #37323 ) ;
#95880=ADVANCED_FACE ( 'NONE', ( #104111 ), #4774, .F. ) ;
#95881=CARTESIAN_POINT ( 'NONE',  ( -34.92500000000001137, -6.048682586364289904, 15.71395525773009538 ) ) ;
#95882=DIRECTION ( 'NONE',  ( -0.7071067811865486830, -0.7071067811865464625, 0.000000000000000000 ) ) ;
#95883=ORIENTED_EDGE ( 'NONE', *, *, #126778, .T. ) ;
#95884=DIRECTION ( 'NONE',  ( 0.6830127018922181881, 0.6830127018922202975, -0.2588190451025214056 ) ) ;
#95885=ORIENTED_EDGE ( 'NONE', *, *, #12263, .F. ) ;
#95886=DIRECTION ( 'NONE',  ( 0.7071067811865487940, 0.7071067811865463515, -0.000000000000000000 ) ) ;
#95887=DIRECTION ( 'NONE',  ( 1.000000000000000000, 0.000000000000000000, 0.000000000000000000 ) ) ;
#95888=LINE ( 'NONE', #42967, #142185 ) ;
#95889=VERTEX_POINT ( 'NONE', #51209 ) ;
#95891=VECTOR ( 'NONE', #129587, 999.9999999999998863 ) ;
#95892=AXIS2_PLACEMENT_3D ( 'NONE', #5903, #72684, #61097 ) ;
#95893=EDGE_CURVE ( 'NONE', #36504, #74632, #39634, .T. ) ;
#95894=CARTESIAN_POINT ( 'NONE',  ( -9.005480084712511157, 28.92564299267931816, 4.000000000000000000 ) ) ;
#95895=LINE ( 'NONE', #141558, #134497 ) ;
#95897=ORIENTED_EDGE ( 'NONE', *, *, #112526, .F. ) ;
#95898=LINE ( 'NONE', #4542, #4453 ) ;
#95901=ADVANCED_FACE ( 'NONE', ( #84558 ), #128750, .F. ) ;
#95902=CARTESIAN_POINT ( 'NONE',  ( 42.48921356237308800, -27.52281430457085065, 5.000000000000000000 ) ) ;
#95903=CARTESIAN_POINT ( 'NONE',  ( -13.49999999999990763, 3.073033219394612825, -6.593910359670999810 ) ) ;
#95904=VECTOR ( 'NONE', #73438, 1000.000000000000000 ) ;
#95906=EDGE_LOOP ( 'NONE', ( #104147, #6129, #74532, #45310 ) ) ;
#95907=LINE ( 'NONE', #74908, #100475 ) ;
#95908=CARTESIAN_POINT ( 'NONE',  ( 0.3281693992235254487, -3.740707523384248390, 4.000000000000000000 ) ) ;
#95910=VECTOR ( 'NONE', #18848, 1000.000000000000000 ) ;
#95912=LINE ( 'NONE', #29225, #15771 ) ;
#95914=DIRECTION ( 'NONE',  ( 0.7071067811865486830, -0.7071067811865464625, -0.000000000000000000 ) ) ;
#95915=PLANE ( 'NONE',  #141720 ) ;
#95918=CARTESIAN_POINT ( 'NONE',  ( 34.49999999999975842, -6.839392718269096783, -8.480912228396162433 ) ) ;
#95919=DIRECTION ( 'NONE',  ( -0.7071067811865486830, -0.7071067811865464625, 0.000000000000000000 ) ) ;
#95920=PLANE ( 'NONE',  #28538 ) ;
#95921=DIRECTION ( 'NONE',  ( 0.7071067811865487940, 0.7071067811865463515, 0.000000000000000000 ) ) ;
#95923=CARTESIAN_POINT ( 'NONE',  ( -13.49999999999990763, 9.431123077392092213, 4.000000000000000000 ) ) ;
#95924=AXIS2_PLACEMENT_3D ( 'NONE', #101742, #45963, #256 ) ;
#95927=ORIENTED_EDGE ( 'NONE', *, *, #111968, .F. ) ;
#95928=ORIENTED_EDGE ( 'NONE', *, *, #22503, .F. ) ;
#95929=DIRECTION ( 'NONE',  ( 0.3543493200069162685, -0.000000000000000000, -0.9351131265310288487 ) ) ;
#95932=FACE_OUTER_BOUND ( 'NONE', #82759, .T. ) ;
#95933=FACE_OUTER_BOUND ( 'NONE', #112177, .T. ) ;
#95934=DIRECTION ( 'NONE',  ( 0.6830127018922180770, -0.6830127018922204085, -0.2588190451025213501 ) ) ;
#95935=EDGE_CURVE ( 'NONE', #127624, #73159, #21430, .T. ) ;
#95936=FACE_OUTER_BOUND ( 'NONE', #82911, .T. ) ;
#95937=DIRECTION ( 'NONE',  ( 0.7071067811865487940, 0.7071067811865463515, 0.000000000000000000 ) ) ;
#95938=EDGE_LOOP ( 'NONE', ( #102493, #68032, #47788, #136151 ) ) ;
#95939=EDGE_CURVE ( 'NONE', #61026, #15122, #19976, .T. ) ;
#95940=CARTESIAN_POINT ( 'NONE',  ( -16.25154412867565412, -11.24070752338416845, 10.39518518046013007 ) ) ;
#95942=CARTESIAN_POINT ( 'NONE',  ( 8.999999999999937828, -8.731860332648835765, -2.120594902707516383 ) ) ;
#95943=CARTESIAN_POINT ( 'NONE',  ( 8.999999999999934275, -16.60178936734447674, 0.8616154019347707083 ) ) ;
#95944=DIRECTION ( 'NONE',  ( -0.6830127018922181881, 0.6830127018922202975, -0.2588190451025214056 ) ) ;
#95945=PLANE ( 'NONE',  #119758 ) ;
#95947=DIRECTION ( 'NONE',  ( -0.7071067811865486830, -0.7071067811865464625, 0.000000000000000000 ) ) ;
#95949=ORIENTED_EDGE ( 'NONE', *, *, #107981, .F. ) ;
#95951=DIRECTION ( 'NONE',  ( 0.7071067811865486830, -0.7071067811865464625, -0.000000000000000000 ) ) ;
#95952=CARTESIAN_POINT ( 'NONE',  ( 45.18398860626900415, 28.73617430169818832, 5.000000000000000000 ) ) ;
#95953=VERTEX_POINT ( 'NONE', #74396 ) ;
#95956=EDGE_CURVE ( 'NONE', #78104, #7710, #97543, .T. ) ;
#95958=VERTEX_POINT ( 'NONE', #109137 ) ;
#95960=ORIENTED_EDGE ( 'NONE', *, *, #15363, .F. ) ;
#95963=LINE ( 'NONE', #74230, #134613 ) ;
#95964=ORIENTED_EDGE ( 'NONE', *, *, #42239, .T. ) ;
#95965=EDGE_CURVE ( 'NONE', #101509, #16508, #41751, .T. ) ;
#95966=DIRECTION ( 'NONE',  ( -0.3543493200069162685, -0.000000000000000000, -0.9351131265310288487 ) ) ;
#95967=CARTESIAN_POINT ( 'NONE',  ( -5.999999999999956479, -8.151047557385073361, -8.977947279169784522 ) ) ;
#95968=VERTEX_POINT ( 'NONE', #19282 ) ;
#95969=CARTESIAN_POINT ( 'NONE',  ( -14.99999999999988098, 17.58746187583906462, 4.000000000000000000 ) ) ;
#95970=DIRECTION ( 'NONE',  ( -0.7071067811865487940, 0.7071067811865463515, -0.000000000000000000 ) ) ;
#95971=LINE ( 'NONE', #51788, #5473 ) ;
#95972=VECTOR ( 'NONE', #72749, 1000.000000000000000 ) ;
#95973=CARTESIAN_POINT ( 'NONE',  ( 5.999999999999955591, -21.03360074219752462, 5.000000000000000000 ) ) ;
#95974=ORIENTED_EDGE ( 'NONE', *, *, #13155, .T. ) ;
#95975=AXIS2_PLACEMENT_3D ( 'NONE', #63011, #141238, #138403 ) ;
#95976=ORIENTED_EDGE ( 'NONE', *, *, #57602, .T. ) ;
#95979=CIRCLE ( 'NONE', #133075, 5.968999999999998529 ) ;
#95981=DIRECTION ( 'NONE',  ( 0.3543493200069162685, -0.000000000000000000, -0.9351131265310288487 ) ) ;
#95983=VERTEX_POINT ( 'NONE', #140345 ) ;
#95984=VERTEX_POINT ( 'NONE', #30892 ) ;
#95985=PLANE ( 'NONE',  #30652 ) ;
#95987=ORIENTED_EDGE ( 'NONE', *, *, #793, .T. ) ;
#95989=EDGE_CURVE ( 'NONE', #74817, #138852, #118584, .T. ) ;
#95990=LINE ( 'NONE', #138814, #18908 ) ;
#95992=LINE ( 'NONE', #140236, #48021 ) ;
#95993=EDGE_CURVE ( 'NONE', #58586, #72242, #142738, .T. ) ;
#95995=FACE_BOUND ( 'NONE', #75497, .T. ) ;
#95996=FACE_OUTER_BOUND ( 'NONE', #33479, .T. ) ;
#95997=EDGE_CURVE ( 'NONE', #127570, #9887, #9823, .T. ) ;
#95998=CARTESIAN_POINT ( 'NONE',  ( -18.48921356237309510, -27.52281430457068367, 5.000000000000000000 ) ) ;
#95999=DIRECTION ( 'NONE',  ( -0.000000000000000000, -0.3543493200069152693, 0.9351131265310292928 ) ) ;
#96000=DIRECTION ( 'NONE',  ( -0.000000000000000000, 0.3543493200069153248, 0.9351131265310292928 ) ) ;
#96001=EDGE_LOOP ( 'NONE', ( #29724, #102804, #26535, #60985 ) ) ;
#96002=DIRECTION ( 'NONE',  ( -0.7071067811865486830, -0.7071067811865464625, 0.000000000000000000 ) ) ;
#96003=VECTOR ( 'NONE', #48906, 1000.000000000000000 ) ;
#96005=EDGE_CURVE ( 'NONE', #63804, #65772, #75122, .T. ) ;
#96007=AXIS2_PLACEMENT_3D ( 'NONE', #78192, #111514, #12194 ) ;
#96009=ORIENTED_EDGE ( 'NONE', *, *, #140825, .T. ) ;
#96012=EDGE_CURVE ( 'NONE', #20530, #50020, #107704, .T. ) ;
#96014=DIRECTION ( 'NONE',  ( -0.6830127018922180770, -0.6830127018922204085, -0.2588190451025213501 ) ) ;
#96015=EDGE_CURVE ( 'NONE', #94037, #108205, #54095, .T. ) ;
#96016=DIRECTION ( 'NONE',  ( 1.000000000000000000, 0.000000000000000000, 0.000000000000000000 ) ) ;
#96017=EDGE_CURVE ( 'NONE', #14271, #10755, #31596, .T. ) ;
#96018=CARTESIAN_POINT ( 'NONE',  ( 0.000000000000000000, 0.000000000000000000, 5.000000000000000000 ) ) ;
#96019=FACE_OUTER_BOUND ( 'NONE', #7295, .T. ) ;
#96020=EDGE_CURVE ( 'NONE', #63701, #9606, #77269, .T. ) ;
#96021=PLANE ( 'NONE',  #10673 ) ;
#96022=CARTESIAN_POINT ( 'NONE',  ( 30.99507522778786850, -5.240707523384228850, 12.38332538355488843 ) ) ;
#96023=DIRECTION ( 'NONE',  ( 0.7071067811865487940, 0.7071067811865463515, 0.000000000000000000 ) ) ;
#96024=CARTESIAN_POINT ( 'NONE',  ( -27.70612307739176572, 22.22500000000000142, 4.000000000000000000 ) ) ;
#96025=DIRECTION ( 'NONE',  ( 0.7071067811865487940, -0.7071067811865463515, 0.000000000000000000 ) ) ;
#96026=VERTEX_POINT ( 'NONE', #87406 ) ;
#96027=DIRECTION ( 'NONE',  ( 0.7071067811865486830, -0.7071067811865464625, -0.000000000000000000 ) ) ;
#96028=CARTESIAN_POINT ( 'NONE',  ( 28.49999999999981171, -1.912538124160733766, 4.000000000000000000 ) ) ;
#96029=EDGE_CURVE ( 'NONE', #31980, #49135, #85236, .T. ) ;
#96030=ORIENTED_EDGE ( 'NONE', *, *, #124732, .F. ) ;
#96031=EDGE_LOOP ( 'NONE', ( #95846, #58479, #36852, #8138 ) ) ;
#96032=ADVANCED_FACE ( 'NONE', ( #51928 ), #129459, .F. ) ;
#96035=ORIENTED_EDGE ( 'NONE', *, *, #101062, .F. ) ;
#96036=CARTESIAN_POINT ( 'NONE',  ( -24.70710678118636494, -9.740707523384187994, 5.000000000000000000 ) ) ;
#96037=EDGE_CURVE ( 'NONE', #114295, #28826, #122141, .T. ) ;
#96041=CARTESIAN_POINT ( 'NONE',  ( -0.7928932188134442116, -2.240707523384266153, 5.000000000000000000 ) ) ;
#96043=DIRECTION ( 'NONE',  ( 0.000000000000000000, 1.000000000000000000, 0.000000000000000000 ) ) ;
#96045=DIRECTION ( 'NONE',  ( 0.000000000000000000, -0.000000000000000000, 1.000000000000000000 ) ) ;
#96046=ORIENTED_EDGE ( 'NONE', *, *, #128705, .F. ) ;
#96047=VERTEX_POINT ( 'NONE', #22806 ) ;
#96048=FACE_OUTER_BOUND ( 'NONE', #111745, .T. ) ;
#96049=ORIENTED_EDGE ( 'NONE', *, *, #38930, .T. ) ;
#96050=PLANE ( 'NONE',  #18029 ) ;
#96051=EDGE_LOOP ( 'NONE', ( #107274, #94262, #107814, #10958 ) ) ;
#96052=EDGE_LOOP ( 'NONE', ( #81787, #13404, #125739, #82438 ) ) ;
#96053=ORIENTED_EDGE ( 'NONE', *, *, #104905, .F. ) ;
#96054=EDGE_CURVE ( 'NONE', #49766, #30783, #115424, .T. ) ;
#96056=DIRECTION ( 'NONE',  ( 1.000000000000000000, 0.000000000000000000, 0.000000000000000000 ) ) ;
#96057=LINE ( 'NONE', #30844, #123209 ) ;
#96058=CARTESIAN_POINT ( 'NONE',  ( -21.29974487139158512, -27.71228299555221142, 4.000000000000000000 ) ) ;
#96060=VERTEX_POINT ( 'NONE', #88845 ) ;
#96061=CARTESIAN_POINT ( 'NONE',  ( 34.49999999999976552, 0.4497235411627803492, -5.599840258123462533 ) ) ;
#96062=ORIENTED_EDGE ( 'NONE', *, *, #130400, .T. ) ;
#96063=LINE ( 'NONE', #39584, #116518 ) ;
#96064=ADVANCED_FACE ( 'NONE', ( #100423 ), #78665, .T. ) ;
#96067=CARTESIAN_POINT ( 'NONE',  ( 0.000000000000000000, 21.72500000000000142, 4.500000000000000888 ) ) ;
#96068=EDGE_LOOP ( 'NONE', ( #129387, #115092, #28943, #64091 ) ) ;
#96069=CARTESIAN_POINT ( 'NONE',  ( 36.66846741159834266, -18.74070752338409562, 20.73178291233849890 ) ) ;
#96071=VERTEX_POINT ( 'NONE', #112018 ) ;
#96073=ORIENTED_EDGE ( 'NONE', *, *, #10366, .F. ) ;
#96074=EDGE_CURVE ( 'NONE', #40937, #11091, #113410, .T. ) ;
#96076=PLANE ( 'NONE',  #39447 ) ;
#96077=DIRECTION ( 'NONE',  ( -0.000000000000000000, 0.000000000000000000, 1.000000000000000000 ) ) ;
#96078=LINE ( 'NONE', #134452, #23777 ) ;
#96082=LINE ( 'NONE', #140321, #120500 ) ;
#96083=DIRECTION ( 'NONE',  ( 0.7071067811865486830, -0.7071067811865464625, -0.000000000000000000 ) ) ;
#96084=VECTOR ( 'NONE', #137674, 1000.000000000000227 ) ;
#96086=EDGE_CURVE ( 'NONE', #138835, #131561, #133071, .T. ) ;
#96087=CARTESIAN_POINT ( 'NONE',  ( 66.18398860626901126, 28.73617430169833753, 5.000000000000000000 ) ) ;
#96088=AXIS2_PLACEMENT_3D ( 'NONE', #95078, #127740, #129142 ) ;
#96089=ORIENTED_EDGE ( 'NONE', *, *, #47458, .T. ) ;
#96090=FACE_OUTER_BOUND ( 'NONE', #118386, .T. ) ;
#96091=EDGE_LOOP ( 'NONE', ( #58507, #102434, #76693, #119429 ) ) ;
#96092=DIRECTION ( 'NONE',  ( 0.3543493200069162685, -0.000000000000000000, -0.9351131265310288487 ) ) ;
#96093=DIRECTION ( 'NONE',  ( 1.000000000000000000, 0.000000000000000000, 0.000000000000000000 ) ) ;
#96094=ORIENTED_EDGE ( 'NONE', *, *, #18257, .F. ) ;
#96095=DIRECTION ( 'NONE',  ( -0.7071067811865487940, 0.7071067811865463515, 0.000000000000000000 ) ) ;
#96097=ORIENTED_EDGE ( 'NONE', *, *, #64994, .T. ) ;
#96100=EDGE_LOOP ( 'NONE', ( #108864, #10579, #15719, #40871 ) ) ;
#96101=ORIENTED_EDGE ( 'NONE', *, *, #121567, .T. ) ;
#96102=DIRECTION ( 'NONE',  ( 0.7071067811865487940, 0.7071067811865463515, -0.000000000000000000 ) ) ;
#96103=DIRECTION ( 'NONE',  ( -0.7071067811865487940, 0.7071067811865463515, 0.000000000000000000 ) ) ;
#96104=CARTESIAN_POINT ( 'NONE',  ( -34.92500000000001137, 1.077975372831878387, 13.01339814852643606 ) ) ;
#96108=EDGE_CURVE ( 'NONE', #64975, #32966, #80819, .T. ) ;
#96109=AXIS2_PLACEMENT_3D ( 'NONE', #58502, #114245, #72766 ) ;
#96110=CARTESIAN_POINT ( 'NONE',  ( -9.918025652846569784, 22.22500000000000142, -4.476077389926565786 ) ) ;
#96113=LINE ( 'NONE', #41754, #28372 ) ;
#96114=FACE_OUTER_BOUND ( 'NONE', #33601, .T. ) ;
#96115=DIRECTION ( 'NONE',  ( -0.3543493200069162685, -0.000000000000000000, -0.9351131265310288487 ) ) ;
#96116=DIRECTION ( 'NONE',  ( -0.7071067811865486830, -0.7071067811865464625, -0.000000000000000000 ) ) ;
#96117=ORIENTED_EDGE ( 'NONE', *, *, #62909, .T. ) ;
#96119=LINE ( 'NONE', #19292, #134817 ) ;
#96120=VERTEX_POINT ( 'NONE', #135894 ) ;
#96121=EDGE_CURVE ( 'NONE', #98171, #102894, #56940, .T. ) ;
#96123=CARTESIAN_POINT ( 'NONE',  ( 10.49999999999992895, 7.466399257802187606, 5.000000000000000000 ) ) ;
#96124=PLANE ( 'NONE',  #649 ) ;
#96125=VERTEX_POINT ( 'NONE', #44652 ) ;
#96126=CARTESIAN_POINT ( 'NONE',  ( -34.92500000000001137, 22.22500000000000142, 0.4999999999999995559 ) ) ;
#96127=LINE ( 'NONE', #54112, #132242 ) ;
#96129=EDGE_CURVE ( 'NONE', #90375, #132873, #55497, .T. ) ;
#96130=LINE ( 'NONE', #41055, #110042 ) ;
#96135=DIRECTION ( 'NONE',  ( -0.7071067811865486830, -0.7071067811865464625, -0.000000000000000000 ) ) ;
#96139=ORIENTED_EDGE ( 'NONE', *, *, #26958, .F. ) ;
#96141=CARTESIAN_POINT ( 'NONE',  ( 5.206660635421493488, 21.75929247661549937, 4.998822639870701856 ) ) ;
#96143=DIRECTION ( 'NONE',  ( 0.000000000000000000, 1.000000000000000000, 0.000000000000000000 ) ) ;
#96144=ORIENTED_EDGE ( 'NONE', *, *, #62882, .T. ) ;
#96145=FACE_OUTER_BOUND ( 'NONE', #75723, .T. ) ;
#96147=ORIENTED_EDGE ( 'NONE', *, *, #76814, .T. ) ;
#96149=CARTESIAN_POINT ( 'NONE',  ( 34.42499999999998295, 22.22500000000000142, 5.000000000000000000 ) ) ;
#96150=CARTESIAN_POINT ( 'NONE',  ( -8.671830600776406328, 8.259292476615634371, 4.000000000000000000 ) ) ;
#96151=( BOUNDED_CURVE ( )  B_SPLINE_CURVE ( 3, ( #44595, #93047, #126378, #103198 ),
 .UNSPECIFIED., .F., .F. ) 
 B_SPLINE_CURVE_WITH_KNOTS ( ( 4, 4 ),
 ( 5.920967161967928050, 7.341195215986584977 ),
 .UNSPECIFIED. ) 
 CURVE ( )  GEOMETRIC_REPRESENTATION_ITEM ( )  RATIONAL_B_SPLINE_CURVE ( ( 1.000000000000000000, 0.8388583629366730410, 0.8388583629366730410, 1.000000000000000000 ) ) 
 REPRESENTATION_ITEM ( '' )  );
#96152=VERTEX_POINT ( 'NONE', #67080 ) ;
#96153=ORIENTED_EDGE ( 'NONE', *, *, #138619, .T. ) ;
#96154=CARTESIAN_POINT ( 'NONE',  ( -31.49999999999976552, 13.46639925780212366, 5.000000000000000000 ) ) ;
#96157=LINE ( 'NONE', #19339, #132348 ) ;
#96158=CARTESIAN_POINT ( 'NONE',  ( 15.48921356237309510, -27.52281430457066236, 5.000000000000000000 ) ) ;
#96161=AXIS2_PLACEMENT_3D ( 'NONE', #65536, #21976, #134893 ) ;
#96162=ORIENTED_EDGE ( 'NONE', *, *, #118394, .T. ) ;
#96163=EDGE_CURVE ( 'NONE', #107639, #110076, #13371, .T. ) ;
#96165=ORIENTED_EDGE ( 'NONE', *, *, #51253, .F. ) ;
#96167=AXIS2_PLACEMENT_3D ( 'NONE', #132403, #34480, #56973 ) ;
#96168=ORIENTED_EDGE ( 'NONE', *, *, #48911, .F. ) ;
#96169=ADVANCED_FACE ( 'NONE', ( #35902 ), #22117, .F. ) ;
#96171=EDGE_CURVE ( 'NONE', #139774, #114801, #80119, .T. ) ;
#96172=DIRECTION ( 'NONE',  ( -0.7071067811865487940, 0.7071067811865463515, 0.000000000000000000 ) ) ;
#96173=EDGE_LOOP ( 'NONE', ( #51460, #132015, #30285, #71874 ) ) ;
#96174=DIRECTION ( 'NONE',  ( -0.7071067811865486830, -0.7071067811865464625, 0.000000000000000000 ) ) ;
#96175=LINE ( 'NONE', #86770, #28812 ) ;
#96176=CARTESIAN_POINT ( 'NONE',  ( 31.49999999999977973, 14.14708470758593784, -0.5283514160167287477 ) ) ;
#96178=LINE ( 'NONE', #62894, #30623 ) ;
#96179=ORIENTED_EDGE ( 'NONE', *, *, #39137, .F. ) ;
#96180=CARTESIAN_POINT ( 'NONE',  ( -15.48921356237309510, -27.52281430457066236, 5.000000000000000000 ) ) ;
#96181=DIRECTION ( 'NONE',  ( -0.7071067811865486830, -0.7071067811865464625, 0.000000000000000000 ) ) ;
#96182=EDGE_CURVE ( 'NONE', #109319, #132339, #124302, .T. ) ;
#96183=ORIENTED_EDGE ( 'NONE', *, *, #29849, .F. ) ;
#96184=CARTESIAN_POINT ( 'NONE',  ( -34.92500000000001137, -22.22500000000000142, 4.000000000000000000 ) ) ;
#96186=ADVANCED_FACE ( 'NONE', ( #11956 ), #101112, .F. ) ;
#96187=CARTESIAN_POINT ( 'NONE',  ( -19.05000000000000071, 3.174999999999997158, 5.000000000000000000 ) ) ;
#96190=ORIENTED_EDGE ( 'NONE', *, *, #32992, .T. ) ;
#96192=EDGE_CURVE ( 'NONE', #41713, #69496, #79427, .T. ) ;
#96193=AXIS2_PLACEMENT_3D ( 'NONE', #100619, #36086, #102038 ) ;
#96194=CARTESIAN_POINT ( 'NONE',  ( -27.18398860626900060, 28.73617430169806042, 5.000000000000000000 ) ) ;
#96196=FACE_OUTER_BOUND ( 'NONE', #108568, .T. ) ;
#96198=DIRECTION ( 'NONE',  ( -0.7071067811865486830, -0.7071067811865464625, -0.000000000000000000 ) ) ;
#96199=VECTOR ( 'NONE', #81295, 1000.000000000000227 ) ;
#96200=CARTESIAN_POINT ( 'NONE',  ( -28.49999999999980460, 12.05218569542904739, 5.000000000000000000 ) ) ;
#96201=ADVANCED_FACE ( 'NONE', ( #104683 ), #83685, .F. ) ;
#96202=CARTESIAN_POINT ( 'NONE',  ( -14.99999999999989875, -1.209798855135683748, 4.371887122346860721 ) ) ;
#96203=VECTOR ( 'NONE', #86120, 1000.000000000000000 ) ;
#96204=DIRECTION ( 'NONE',  ( -0.7071067811865486830, -0.7071067811865464625, 0.000000000000000000 ) ) ;
#96205=DIRECTION ( 'NONE',  ( 0.7071067811865487940, 0.7071067811865463515, -0.000000000000000000 ) ) ;
#96207=VERTEX_POINT ( 'NONE', #25693 ) ;
#96208=ORIENTED_EDGE ( 'NONE', *, *, #122558, .T. ) ;
#96210=ORIENTED_EDGE ( 'NONE', *, *, #48553, .T. ) ;
#96211=EDGE_CURVE ( 'NONE', #113151, #125882, #71361, .T. ) ;
#96213=FACE_OUTER_BOUND ( 'NONE', #38253, .T. ) ;
#96214=CARTESIAN_POINT ( 'NONE',  ( -0.3281693992235271695, 20.25929247661551003, 4.000000000000000000 ) ) ;
#96215=DIRECTION ( 'NONE',  ( 1.000000000000000000, 0.000000000000000000, 0.000000000000000000 ) ) ;
#96216=ORIENTED_EDGE ( 'NONE', *, *, #117251, .F. ) ;
#96220=CARTESIAN_POINT ( 'NONE',  ( -5.700255128608413102, -27.71228299555201957, 4.000000000000000000 ) ) ;
#96221=CARTESIAN_POINT ( 'NONE',  ( 8.673617379884035472E-16, -21.84840872380824450, 2.849755605029608230 ) ) ;
#96224=ORIENTED_EDGE ( 'NONE', *, *, #40086, .F. ) ;
#96225=EDGE_CURVE ( 'NONE', #113826, #55035, #16213, .T. ) ;
#96226=ORIENTED_EDGE ( 'NONE', *, *, #113858, .F. ) ;
#96227=PLANE ( 'NONE',  #7852 ) ;
#96229=DIRECTION ( 'NONE',  ( -0.7071067811865486830, -0.7071067811865464625, 0.000000000000000000 ) ) ;
#96230=LINE ( 'NONE', #119412, #45040 ) ;
#96231=DIRECTION ( 'NONE',  ( -0.7071067811865486830, -0.7071067811865464625, 0.000000000000000000 ) ) ;
#96232=LINE ( 'NONE', #75945, #24849 ) ;
#96235=ADVANCED_FACE ( 'NONE', ( #115519 ), #72833, .F. ) ;
#96237=EDGE_LOOP ( 'NONE', ( #121650, #17452, #43804, #33498 ) ) ;
#96238=DIRECTION ( 'NONE',  ( -0.000000000000000000, 0.000000000000000000, 1.000000000000000000 ) ) ;
#96239=DIRECTION ( 'NONE',  ( -0.3543493200069163240, 0.000000000000000000, 0.9351131265310288487 ) ) ;
#96240=EDGE_LOOP ( 'NONE', ( #113925, #42336, #5550, #86196 ) ) ;
#96241=CARTESIAN_POINT ( 'NONE',  ( -28.49999999999979750, -4.912538124160708897, 4.000000000000000000 ) ) ;
#96243=ORIENTED_EDGE ( 'NONE', *, *, #23829, .T. ) ;
#96244=EDGE_CURVE ( 'NONE', #69882, #1156, #48173, .T. ) ;
#96245=DIRECTION ( 'NONE',  ( 0.7071067811865487940, -0.7071067811865463515, 0.000000000000000000 ) ) ;
#96247=ORIENTED_EDGE ( 'NONE', *, *, #8932, .T. ) ;
#96248=CARTESIAN_POINT ( 'NONE',  ( -12.48921356237309155, -27.52281430457064104, 5.000000000000000000 ) ) ;
#96249=ORIENTED_EDGE ( 'NONE', *, *, #43491, .T. ) ;
#96250=CARTESIAN_POINT ( 'NONE',  ( -18.70710678118641468, 20.25929247661551713, 5.000000000000000000 ) ) ;
#96251=AXIS2_PLACEMENT_3D ( 'NONE', #52125, #85445, #129673 ) ;
#96253=CARTESIAN_POINT ( 'NONE',  ( -34.49999999999975131, -4.912538124160707120, 4.000000000000000000 ) ) ;
#96254=CARTESIAN_POINT ( 'NONE',  ( 35.71998032010574775, 0.7592924766157138627, 14.27032725228017185 ) ) ;
#96255=DIRECTION ( 'NONE',  ( -0.7071067811865487940, 0.7071067811865463515, -0.000000000000000000 ) ) ;
#96256=EDGE_CURVE ( 'NONE', #37537, #39265, #60504, .T. ) ;
#96262=LINE ( 'NONE', #63700, #3774 ) ;
#96264=ORIENTED_EDGE ( 'NONE', *, *, #116362, .T. ) ;
#96265=VERTEX_POINT ( 'NONE', #17654 ) ;
#96267=VECTOR ( 'NONE', #86513, 999.9999999999998863 ) ;
#96268=CARTESIAN_POINT ( 'NONE',  ( 13.49999999999990585, 16.77039438581780217, 0.4657186855307419160 ) ) ;
#96269=PLANE ( 'NONE',  #101804 ) ;
#96270=CARTESIAN_POINT ( 'NONE',  ( 8.343289998337821700, 3.759292476615681888, 13.27625715073267543 ) ) ;
#96272=VERTEX_POINT ( 'NONE', #61927 ) ;
#96273=DIRECTION ( 'NONE',  ( -0.6830127018922180770, -0.6830127018922204085, -0.2588190451025213501 ) ) ;
#96274=DIRECTION ( 'NONE',  ( -0.6830127018922181881, 0.6830127018922202975, -0.2588190451025214056 ) ) ;
#96275=LINE ( 'NONE', #40525, #25689 ) ;
#96277=EDGE_CURVE ( 'NONE', #85340, #50158, #49634, .T. ) ;
#96278=DIRECTION ( 'NONE',  ( 0.3543493200069163240, -0.000000000000000000, -0.9351131265310288487 ) ) ;
#96279=DIRECTION ( 'NONE',  ( 0.7071067811865487940, -0.7071067811865463515, 0.000000000000000000 ) ) ;
#96280=EDGE_LOOP ( 'NONE', ( #20909, #121368, #96815, #38815 ) ) ;
#96281=LINE ( 'NONE', #140524, #83665 ) ;
#96282=CARTESIAN_POINT ( 'NONE',  ( -8.999999999999934275, -21.41253812416053748, 4.000000000000000000 ) ) ;
#96283=DIRECTION ( 'NONE',  ( -0.7071067811865487940, 0.7071067811865463515, 0.000000000000000000 ) ) ;
#96284=CARTESIAN_POINT ( 'NONE',  ( 2.999999999999988898, 1.552185695429151080, 5.000000000000000000 ) ) ;
#96285=FACE_OUTER_BOUND ( 'NONE', #124415, .T. ) ;
#96286=VECTOR ( 'NONE', #34300, 1000.000000000000000 ) ;
#96289=ORIENTED_EDGE ( 'NONE', *, *, #78088, .T. ) ;
#96290=VERTEX_POINT ( 'NONE', #92361 ) ;
#96293=ORIENTED_EDGE ( 'NONE', *, *, #71799, .F. ) ;
#96294=VECTOR ( 'NONE', #35570, 1000.000000000000000 ) ;
#96296=VECTOR ( 'NONE', #58007, 1000.000000000000000 ) ;
#96297=CARTESIAN_POINT ( 'NONE',  ( -2.207106781186529698, 18.75929247661552779, 5.000000000000000000 ) ) ;
#96299=ADVANCED_FACE ( 'NONE', ( #38725 ), #26424, .T. ) ;
#96300=FACE_OUTER_BOUND ( 'NONE', #53766, .T. ) ;
#96301=DIRECTION ( 'NONE',  ( 0.7071067811865487940, 0.7071067811865463515, 0.000000000000000000 ) ) ;
#96303=ORIENTED_EDGE ( 'NONE', *, *, #54310, .F. ) ;
#96304=DIRECTION ( 'NONE',  ( 0.7071067811865486830, -0.7071067811865464625, -0.000000000000000000 ) ) ;
#96305=DIRECTION ( 'NONE',  ( -0.7071067811865486830, -0.7071067811865464625, 0.000000000000000000 ) ) ;
#96306=CARTESIAN_POINT ( 'NONE',  ( 34.92499999999998295, 15.00612307739180551, 4.000000000000000000 ) ) ;
#96307=PLANE ( 'NONE',  #4438 ) ;
#96309=ORIENTED_EDGE ( 'NONE', *, *, #27667, .T. ) ;
#96310=EDGE_LOOP ( 'NONE', ( #92901, #64855, #9274, #26552 ) ) ;
#96311=LINE ( 'NONE', #52820, #134809 ) ;
#96312=DIRECTION ( 'NONE',  ( 0.6830127018922180770, -0.6830127018922204085, -0.2588190451025213501 ) ) ;
#96314=DIRECTION ( 'NONE',  ( -0.7071067811865486830, -0.7071067811865464625, -0.000000000000000000 ) ) ;
#96316=EDGE_CURVE ( 'NONE', #90677, #74481, #15498, .T. ) ;
#96318=VERTEX_POINT ( 'NONE', #40186 ) ;
#96319=EDGE_CURVE ( 'NONE', #92143, #111424, #125011, .T. ) ;
#96320=CARTESIAN_POINT ( 'NONE',  ( 12.70710678118645554, -18.74070752338409562, 5.000000000000000000 ) ) ;
#96321=ORIENTED_EDGE ( 'NONE', *, *, #136588, .T. ) ;
#96322=EDGE_LOOP ( 'NONE', ( #110414, #33588, #98518, #46927 ) ) ;
#96324=EDGE_CURVE ( 'NONE', #138495, #108055, #37297, .T. ) ;
#96326=FACE_OUTER_BOUND ( 'NONE', #141865, .T. ) ;
#96327=CARTESIAN_POINT ( 'NONE',  ( -33.48921356237309510, -27.52281430457078670, 5.000000000000000000 ) ) ;
#96331=CARTESIAN_POINT ( 'NONE',  ( 1.499999999999994449, -13.91253812416061564, 4.000000000000000000 ) ) ;
#96335=ORIENTED_EDGE ( 'NONE', *, *, #80293, .T. ) ;
#96336=CARTESIAN_POINT ( 'NONE',  ( 16.49999999999988987, -5.947814304570758104, 5.000000000000000000 ) ) ;
#96338=EDGE_CURVE ( 'NONE', #22961, #36965, #48899, .T. ) ;
#96339=EDGE_LOOP ( 'NONE', ( #63978, #137859, #101521, #84236 ) ) ;
#96342=CARTESIAN_POINT ( 'NONE',  ( -41.99451991528749062, 28.92564299267967343, 4.000000000000000000 ) ) ;
#96343=EDGE_CURVE ( 'NONE', #125425, #117394, #38029, .T. ) ;
#96344=EDGE_LOOP ( 'NONE', ( #69389, #55312, #4427, #10076 ) ) ;
#96345=CARTESIAN_POINT ( 'NONE',  ( -11.99999999999990941, 4.552185695429119328, 5.000000000000000000 ) ) ;
#96347=EDGE_LOOP ( 'NONE', ( #45441, #94331, #73724, #101113 ) ) ;
#96348=ORIENTED_EDGE ( 'NONE', *, *, #54022, .T. ) ;
#96349=EDGE_CURVE ( 'NONE', #49447, #97071, #76354, .T. ) ;
#96351=FACE_OUTER_BOUND ( 'NONE', #142927, .T. ) ;
#96352=ADVANCED_FACE ( 'NONE', ( #32126 ), #73504, .F. ) ;
#96354=CARTESIAN_POINT ( 'NONE',  ( 36.18398860626899705, 28.73617430169812437, 5.000000000000000000 ) ) ;
#96356=CARTESIAN_POINT ( 'NONE',  ( -18.48921356237309510, -27.52281430457068367, 5.000000000000000000 ) ) ;
#96357=CARTESIAN_POINT ( 'NONE',  ( 34.17183060077623225, -5.240707523384234179, 4.000000000000000000 ) ) ;
#96358=CARTESIAN_POINT ( 'NONE',  ( 9.183988606268997046, 28.73617430169793607, 5.000000000000000000 ) ) ;
#96359=DIRECTION ( 'NONE',  ( -0.7071067811865486830, -0.7071067811865464625, -0.000000000000000000 ) ) ;
#96360=CARTESIAN_POINT ( 'NONE',  ( 19.49999999999986500, -4.216083040037233332, -7.486842126848701540 ) ) ;
#96361=EDGE_CURVE ( 'NONE', #40163, #72227, #29262, .T. ) ;
#96362=DIRECTION ( 'NONE',  ( -0.7071067811865487940, 0.7071067811865463515, -0.000000000000000000 ) ) ;
#96363=CARTESIAN_POINT ( 'NONE',  ( -20.20710678118640402, 12.75929247661558819, 5.000000000000000000 ) ) ;
#96364=CARTESIAN_POINT ( 'NONE',  ( -34.42500000000001137, -12.02281430457044564, 5.000000000000000000 ) ) ;
#96365=LINE ( 'NONE', #97834, #35584 ) ;
#96366=VECTOR ( 'NONE', #126665, 1000.000000000000000 ) ;
#96367=EDGE_LOOP ( 'NONE', ( #25384, #118839, #17855, #116581 ) ) ;
#96368=ORIENTED_EDGE ( 'NONE', *, *, #126661, .F. ) ;
#96369=EDGE_CURVE ( 'NONE', #90677, #131000, #108216, .T. ) ;
#96370=VERTEX_POINT ( 'NONE', #43018 ) ;
#96371=ORIENTED_EDGE ( 'NONE', *, *, #9246, .T. ) ;
#96372=FACE_OUTER_BOUND ( 'NONE', #66883, .T. ) ;
#96373=ORIENTED_EDGE ( 'NONE', *, *, #64607, .T. ) ;
#96374=ORIENTED_EDGE ( 'NONE', *, *, #44508, .F. ) ;
#96375=PLANE ( 'NONE',  #44521 ) ;
#96376=CARTESIAN_POINT ( 'NONE',  ( 16.49999999999988276, -12.08601207473287964, -10.46905243149098119 ) ) ;
#96377=VECTOR ( 'NONE', #2533, 1000.000000000000000 ) ;
#96378=FACE_OUTER_BOUND ( 'NONE', #54457, .T. ) ;
#96379=ADVANCED_FACE ( 'NONE', ( #117667 ), #119816, .F. ) ;
#96380=ORIENTED_EDGE ( 'NONE', *, *, #3403, .T. ) ;
#96381=EDGE_CURVE ( 'NONE', #124489, #18049, #140183, .T. ) ;
#96382=LINE ( 'NONE', #139952, #81174 ) ;
#96383=ORIENTED_EDGE ( 'NONE', *, *, #9462, .T. ) ;
#96384=VECTOR ( 'NONE', #101689, 1000.000000000000000 ) ;
#96385=VECTOR ( 'NONE', #32166, 1000.000000000000227 ) ;
#96386=CARTESIAN_POINT ( 'NONE',  ( -34.49999999999975842, 15.05432934483078533, 4.994342998332167660 ) ) ;
#96387=ADVANCED_FACE ( 'NONE', ( #119126 ), #7498, .F. ) ;
#96388=CARTESIAN_POINT ( 'NONE',  ( -10.88982677111781427, -22.22500000000000142, 4.785647885939353863 ) ) ;
#96389=AXIS2_PLACEMENT_3D ( 'NONE', #131290, #96480, #140723 ) ;
#96391=ORIENTED_EDGE ( 'NONE', *, *, #96993, .T. ) ;
#96394=DIRECTION ( 'NONE',  ( -0.7071067811865486830, -0.7071067811865464625, 0.000000000000000000 ) ) ;
#96395=DIRECTION ( 'NONE',  ( 0.3543493200069162685, -0.000000000000000000, -0.9351131265310288487 ) ) ;
#96396=EDGE_LOOP ( 'NONE', ( #72598, #118196, #30011, #23691 ) ) ;
#96398=DIRECTION ( 'NONE',  ( 0.7071067811865487940, 0.7071067811865463515, -0.000000000000000000 ) ) ;
#96399=ORIENTED_EDGE ( 'NONE', *, *, #73097, .F. ) ;
#96402=AXIS2_PLACEMENT_3D ( 'NONE', #44830, #9999, #143368 ) ;
#96403=LINE ( 'NONE', #105166, #21474 ) ;
#96404=CARTESIAN_POINT ( 'NONE',  ( -34.92500000000001137, 22.22500000000000142, 4.000000000000000000 ) ) ;
#96406=DIRECTION ( 'NONE',  ( 1.000000000000000000, 0.000000000000000000, 0.000000000000000000 ) ) ;
#96407=LINE ( 'NONE', #117453, #129924 ) ;
#96408=FACE_OUTER_BOUND ( 'NONE', #83950, .T. ) ;
#96410=PLANE ( 'NONE',  #104533 ) ;
#96411=CARTESIAN_POINT ( 'NONE',  ( -2.187538124160505415, -22.22500000000000142, 4.000000000000000000 ) ) ;
#96412=VERTEX_POINT ( 'NONE', #140863 ) ;
#96416=DIRECTION ( 'NONE',  ( 0.7071067811865486830, -0.7071067811865464625, -0.000000000000000000 ) ) ;
#96417=CARTESIAN_POINT ( 'NONE',  ( -36.18398860626899705, 28.73617430169812437, 5.000000000000000000 ) ) ;
#96418=EDGE_LOOP ( 'NONE', ( #112595, #19751, #79723, #40295 ) ) ;
#96419=CARTESIAN_POINT ( 'NONE',  ( 8.999999999999937828, -21.84840872380823740, 2.849755605029629546 ) ) ;
#96420=PLANE ( 'NONE',  #56828 ) ;
#96421=CARTESIAN_POINT ( 'NONE',  ( 6.792893218813407685, 18.75929247661553489, 5.000000000000000000 ) ) ;
#96422=DIRECTION ( 'NONE',  ( -0.7071067811865486830, -0.7071067811865464625, 0.000000000000000000 ) ) ;
#96423=CARTESIAN_POINT ( 'NONE',  ( 34.49999999999975842, 16.46425560840032531, 4.994342998332160555 ) ) ;
#96424=DIRECTION ( 'NONE',  ( -0.000000000000000000, 0.3543493200069153248, 0.9351131265310292928 ) ) ;
#96425=CARTESIAN_POINT ( 'NONE',  ( 34.49999999999975842, 10.46425560840038571, 4.994342998332157890 ) ) ;
#96426=CARTESIAN_POINT ( 'NONE',  ( 17.99999999999987210, 12.83542986846998524, -1.025386466790412454 ) ) ;
#96427=LINE ( 'NONE', #10852, #6237 ) ;
#96429=VECTOR ( 'NONE', #139336, 999.9999999999998863 ) ;
#96430=LINE ( 'NONE', #31230, #8935 ) ;
#96431=CARTESIAN_POINT ( 'NONE',  ( 34.49999999999975131, 13.46425560840035196, 4.994342998332160555 ) ) ;
#96433=ORIENTED_EDGE ( 'NONE', *, *, #80691, .T. ) ;
#96434=ORIENTED_EDGE ( 'NONE', *, *, #101844, .F. ) ;
#96435=EDGE_LOOP ( 'NONE', ( #19346, #114701, #51987, #74937 ) ) ;
#96439=VERTEX_POINT ( 'NONE', #96625 ) ;
#96440=VECTOR ( 'NONE', #139308, 1000.000000000000227 ) ;
#96441=LINE ( 'NONE', #30528, #117455 ) ;
#96442=FACE_OUTER_BOUND ( 'NONE', #34367, .T. ) ;
#96443=ORIENTED_EDGE ( 'NONE', *, *, #18195, .T. ) ;
#96445=CARTESIAN_POINT ( 'NONE',  ( 27.29974487139158512, -27.71228299555225405, 4.000000000000000000 ) ) ;
#96446=FACE_OUTER_BOUND ( 'NONE', #14997, .T. ) ;
#96448=DIRECTION ( 'NONE',  ( -0.7071067811865486830, 0.7071067811865464625, 0.000000000000000000 ) ) ;
#96451=ORIENTED_EDGE ( 'NONE', *, *, #130943, .T. ) ;
#96453=CARTESIAN_POINT ( 'NONE',  ( 17.87852683662842068, -20.24070752338407075, 7.412974875817750053 ) ) ;
#96454=ADVANCED_FACE ( 'NONE', ( #53912 ), #18352, .F. ) ;
#96455=CARTESIAN_POINT ( 'NONE',  ( -15.71462683630238111, 8.126010640810376273, 4.668119888204643075 ) ) ;
#96457=CARTESIAN_POINT ( 'NONE',  ( 22.49999999999985434, -10.53360074219763121, 5.000000000000000000 ) ) ;
#96458=CARTESIAN_POINT ( 'NONE',  ( 39.18398860626899705, 28.73617430169814568, 5.000000000000000000 ) ) ;
#96460=VECTOR ( 'NONE', #102479, 999.9999999999998863 ) ;
#96461=FACE_OUTER_BOUND ( 'NONE', #86426, .T. ) ;
#96462=EDGE_LOOP ( 'NONE', ( #125178, #114584, #16962, #71665 ) ) ;
#96463=ORIENTED_EDGE ( 'NONE', *, *, #118266, .T. ) ;
#96465=VECTOR ( 'NONE', #61298, 1000.000000000000000 ) ;
#96466=ORIENTED_EDGE ( 'NONE', *, *, #9364, .F. ) ;
#96467=EDGE_CURVE ( 'NONE', #44871, #29293, #42315, .T. ) ;
#96468=CARTESIAN_POINT ( 'NONE',  ( 34.92499999999998295, -22.22500000000000142, 4.500000000000000888 ) ) ;
#96471=CARTESIAN_POINT ( 'NONE',  ( -27.79289321881326558, -8.240707523384200428, 5.000000000000000000 ) ) ;
#96472=ADVANCED_FACE ( 'NONE', ( #64049 ), #29968, .T. ) ;
#96473=PLANE ( 'NONE',  #99866 ) ;
#96476=FACE_OUTER_BOUND ( 'NONE', #74314, .T. ) ;
#96477=VERTEX_POINT ( 'NONE', #106809 ) ;
#96478=FACE_OUTER_BOUND ( 'NONE', #12375, .T. ) ;
#96480=DIRECTION ( 'NONE',  ( 0.6830127018922180770, -0.6830127018922204085, -0.2588190451025213501 ) ) ;
#96481=PLANE ( 'NONE',  #64993 ) ;
#96482=VERTEX_POINT ( 'NONE', #118403 ) ;
#96485=ORIENTED_EDGE ( 'NONE', *, *, #128484, .T. ) ;
#96486=LINE ( 'NONE', #42888, #746 ) ;
#96487=DIRECTION ( 'NONE',  ( -0.6830127018922180770, -0.6830127018922204085, -0.2588190451025213501 ) ) ;
#96489=EDGE_CURVE ( 'NONE', #63809, #37645, #87226, .T. ) ;
#96490=LINE ( 'NONE', #40736, #122780 ) ;
#96491=AXIS2_PLACEMENT_3D ( 'NONE', #116853, #17527, #62488 ) ;
#96492=AXIS2_PLACEMENT_3D ( 'NONE', #13771, #104363, #136291 ) ;
#96495=ORIENTED_EDGE ( 'NONE', *, *, #65353, .F. ) ;
#96496=EDGE_CURVE ( 'NONE', #6847, #66027, #97348, .T. ) ;
#96497=VECTOR ( 'NONE', #134634, 999.9999999999998863 ) ;
#96498=DIRECTION ( 'NONE',  ( 0.7071067811865486830, -0.7071067811865464625, -0.000000000000000000 ) ) ;
#96502=ORIENTED_EDGE ( 'NONE', *, *, #130976, .F. ) ;
#96503=EDGE_CURVE ( 'NONE', #29058, #131561, #75644, .T. ) ;
#96504=ADVANCED_FACE ( 'NONE', ( #121968 ), #100247, .F. ) ;
#96505=PLANE ( 'NONE',  #63031 ) ;
#96506=ORIENTED_EDGE ( 'NONE', *, *, #117221, .F. ) ;
#96508=DIRECTION ( 'NONE',  ( -0.7071067811865487940, 0.7071067811865463515, -0.000000000000000000 ) ) ;
#96509=EDGE_CURVE ( 'NONE', #42250, #98347, #46634, .T. ) ;
#96510=DIRECTION ( 'NONE',  ( 0.6830127018922181881, 0.6830127018922202975, -0.2588190451025214056 ) ) ;
#96511=FACE_BOUND ( 'NONE', #15555, .T. ) ;
#96512=EDGE_CURVE ( 'NONE', #8455, #96941, #133598, .T. ) ;
#96513=ORIENTED_EDGE ( 'NONE', *, *, #21329, .F. ) ;
#96514=PLANE ( 'NONE',  #140566 ) ;
#96515=CARTESIAN_POINT ( 'NONE',  ( -2.292893218813431666, 14.25929247661557220, 5.000000000000000000 ) ) ;
#96516=DIRECTION ( 'NONE',  ( -0.7071067811865486830, 0.7071067811865464625, 0.000000000000000000 ) ) ;
#96517=EDGE_CURVE ( 'NONE', #18457, #121677, #135050, .T. ) ;
#96518=ORIENTED_EDGE ( 'NONE', *, *, #111462, .T. ) ;
#96519=DIRECTION ( 'NONE',  ( -0.000000000000000000, -0.3543493200069152138, 0.9351131265310292928 ) ) ;
#96520=ORIENTED_EDGE ( 'NONE', *, *, #129554, .T. ) ;
#96522=VERTEX_POINT ( 'NONE', #34274 ) ;
#96523=CARTESIAN_POINT ( 'NONE',  ( -3.489213562373097322, -27.52281430457057709, 5.000000000000000000 ) ) ;
#96524=ORIENTED_EDGE ( 'NONE', *, *, #8810, .T. ) ;
#96526=VECTOR ( 'NONE', #83562, 1000.000000000000000 ) ;
#96527=EDGE_LOOP ( 'NONE', ( #45100, #17867, #117075, #87995 ) ) ;
#96528=ADVANCED_FACE ( 'NONE', ( #79962 ), #134311, .F. ) ;
#96529=FACE_OUTER_BOUND ( 'NONE', #120827, .T. ) ;
#96530=CARTESIAN_POINT ( 'NONE',  ( -34.92500000000001137, -17.33753812416083306, 4.000000000000000000 ) ) ;
#96531=ORIENTED_EDGE ( 'NONE', *, *, #90256, .T. ) ;
#96532=VECTOR ( 'NONE', #103452, 1000.000000000000000 ) ;
#96533=ADVANCED_FACE ( 'NONE', ( #13203 ), #121269, .F. ) ;
#96535=CARTESIAN_POINT ( 'NONE',  ( 30.48921356237309510, -27.52281430457076894, 5.000000000000000000 ) ) ;
#96536=DIRECTION ( 'NONE',  ( -0.000000000000000000, -0.3543493200069152693, 0.9351131265310292928 ) ) ;
#96537=LINE ( 'NONE', #39364, #52824 ) ;
#96539=LINE ( 'NONE', #41470, #120369 ) ;
#96540=ORIENTED_EDGE ( 'NONE', *, *, #94951, .T. ) ;
#96541=VECTOR ( 'NONE', #7113, 999.9999999999998863 ) ;
#96542=VERTEX_POINT ( 'NONE', #112544 ) ;
#96543=DIRECTION ( 'NONE',  ( -0.7071067811865487940, 0.7071067811865463515, 0.000000000000000000 ) ) ;
#96544=DIRECTION ( 'NONE',  ( 0.7071067811865486830, -0.7071067811865464625, -0.000000000000000000 ) ) ;
#96545=ORIENTED_EDGE ( 'NONE', *, *, #66831, .T. ) ;
#96547=EDGE_LOOP ( 'NONE', ( #101863, #132301, #112465, #7011, #66630, #63997, #100767, #23870, #69671, #37704, #16891, #57622, #2251, #139090, #22736, #49229, #7951, #3607, #12020, #134802, #106716, #30451, #130661, #85281, #89676, #108563, #131475, #128135, #42699, #135640, #136359, #59385, #31113, #8628, #12798, #43175, #50712, #117778 ) ) ;
#96548=VECTOR ( 'NONE', #11295, 1000.000000000000000 ) ;
#96549=DIRECTION ( 'NONE',  ( 0.6830127018922180770, -0.6830127018922204085, -0.2588190451025213501 ) ) ;
#96551=LINE ( 'NONE', #50959, #101851 ) ;
#96552=ADVANCED_FACE ( 'NONE', ( #67649 ), #11774, .T. ) ;
#96553=LINE ( 'NONE', #63296, #135026 ) ;
#96554=ADVANCED_FACE ( 'NONE', ( #77092 ), #124133, .F. ) ;
#96556=LINE ( 'NONE', #133344, #14819 ) ;
#96557=VERTEX_POINT ( 'NONE', #90061 ) ;
#96559=AXIS2_PLACEMENT_3D ( 'NONE', #35790, #110430, #80010 ) ;
#96560=CARTESIAN_POINT ( 'NONE',  ( 44.99451991528749772, 28.92564299267969474, 4.000000000000000000 ) ) ;
#96561=DIRECTION ( 'NONE',  ( 0.7071067811865487940, -0.7071067811865463515, 0.000000000000000000 ) ) ;
#96563=ORIENTED_EDGE ( 'NONE', *, *, #105961, .F. ) ;
#96564=PLANE ( 'NONE',  #41538 ) ;
#96565=ORIENTED_EDGE ( 'NONE', *, *, #96086, .T. ) ;
#96566=LINE ( 'NONE', #53082, #86729 ) ;
#96569=ORIENTED_EDGE ( 'NONE', *, *, #115815, .F. ) ;
#96570=DIRECTION ( 'NONE',  ( -0.000000000000000000, -0.000000000000000000, 1.000000000000000000 ) ) ;
#96572=CARTESIAN_POINT ( 'NONE',  ( -18.48921356237309510, -27.52281430457068367, 5.000000000000000000 ) ) ;
#96573=ORIENTED_EDGE ( 'NONE', *, *, #61617, .T. ) ;
#96575=LINE ( 'NONE', #50987, #125679 ) ;
#96576=CARTESIAN_POINT ( 'NONE',  ( -32.20710678118631165, -17.24070752338410983, 5.000000000000000000 ) ) ;
#96577=VECTOR ( 'NONE', #87974, 1000.000000000000000 ) ;
#96578=DIRECTION ( 'NONE',  ( -0.3543493200069162685, -0.000000000000000000, -0.9351131265310288487 ) ) ;
#96580=VERTEX_POINT ( 'NONE', #12505 ) ;
#96581=PLANE ( 'NONE',  #86615 ) ;
#96582=DIRECTION ( 'NONE',  ( -0.000000000000000000, -0.3543493200069152693, 0.9351131265310292928 ) ) ;
#96583=AXIS2_PLACEMENT_3D ( 'NONE', #108433, #65740, #54831 ) ;
#96586=DIRECTION ( 'NONE',  ( -0.7071067811865486830, -0.7071067811865464625, -0.000000000000000000 ) ) ;
#96588=DIRECTION ( 'NONE',  ( 1.000000000000000000, 0.000000000000000000, 0.000000000000000000 ) ) ;
#96589=DIRECTION ( 'NONE',  ( 1.000000000000000000, 0.000000000000000000, 0.000000000000000000 ) ) ;
#96590=ORIENTED_EDGE ( 'NONE', *, *, #55966, .F. ) ;
#96592=DIRECTION ( 'NONE',  ( 1.000000000000000000, 0.000000000000000000, 0.000000000000000000 ) ) ;
#96594=VECTOR ( 'NONE', #70185, 1000.000000000000227 ) ;
#96595=DIRECTION ( 'NONE',  ( 1.000000000000000000, 0.000000000000000000, 0.000000000000000000 ) ) ;
#96597=CARTESIAN_POINT ( 'NONE',  ( -0.1214731633714660752, -20.24070752338407075, 7.412974875817792686 ) ) ;
#96598=EDGE_LOOP ( 'NONE', ( #8703, #32314, #93499, #90643 ) ) ;
#96601=ORIENTED_EDGE ( 'NONE', *, *, #25620, .T. ) ;
#96602=CARTESIAN_POINT ( 'NONE',  ( 26.99999999999981526, 7.007997736742471062, -8.085015511992050818 ) ) ;
#96603=DIRECTION ( 'NONE',  ( -0.7071067811865486830, 0.7071067811865464625, 0.000000000000000000 ) ) ;
#96604=ORIENTED_EDGE ( 'NONE', *, *, #125721, .T. ) ;
#96605=CARTESIAN_POINT ( 'NONE',  ( -6.183988606268994381, 28.73617430169791476, 5.000000000000000000 ) ) ;
#96606=CARTESIAN_POINT ( 'NONE',  ( 38.99451991528749062, 28.92564299267965211, 4.000000000000000000 ) ) ;
#96607=EDGE_CURVE ( 'NONE', #31098, #93168, #88671, .T. ) ;
#96609=DIRECTION ( 'NONE',  ( -0.7071067811865486830, -0.7071067811865464625, 0.000000000000000000 ) ) ;
#96611=ADVANCED_FACE ( 'NONE', ( #43716 ), #33586, .T. ) ;
#96612=EDGE_CURVE ( 'NONE', #133571, #31974, #79252, .T. ) ;
#96613=ORIENTED_EDGE ( 'NONE', *, *, #79105, .F. ) ;
#96615=CARTESIAN_POINT ( 'NONE',  ( 2.538396446294277631, -9.740707523384180888, 17.74957260769611267 ) ) ;
#96616=AXIS2_PLACEMENT_3D ( 'NONE', #108315, #98892, #10453 ) ;
#96617=DIRECTION ( 'NONE',  ( 0.7071067811865486830, -0.7071067811865464625, -0.000000000000000000 ) ) ;
#96618=LINE ( 'NONE', #77085, #8487 ) ;
#96620=FACE_OUTER_BOUND ( 'NONE', #113731, .T. ) ;
#96621=EDGE_CURVE ( 'NONE', #54679, #33281, #66201, .T. ) ;
#96624=VECTOR ( 'NONE', #96936, 999.9999999999998863 ) ;
#96625=CARTESIAN_POINT ( 'NONE',  ( -13.49999999999990052, 16.46639925780209168, 5.000000000000000000 ) ) ;
#96626=EDGE_LOOP ( 'NONE', ( #98207, #47008, #135575 ) ) ;
#96629=DIRECTION ( 'NONE',  ( 0.6830127018922181881, 0.6830127018922202975, -0.2588190451025214056 ) ) ;
#96630=EDGE_CURVE ( 'NONE', #139000, #101542, #2316, .T. ) ;
#96631=FACE_OUTER_BOUND ( 'NONE', #16467, .T. ) ;
#96632=DIRECTION ( 'NONE',  ( -0.7071067811865486830, -0.7071067811865464625, 0.000000000000000000 ) ) ;
#96634=CARTESIAN_POINT ( 'NONE',  ( -10.49999999999992006, 0.05218569542917404769, 5.000000000000000000 ) ) ;
#96635=EDGE_CURVE ( 'NONE', #70864, #22430, #44464, .T. ) ;
#96637=EDGE_LOOP ( 'NONE', ( #86335, #131053, #46521, #109995 ) ) ;
#96638=EDGE_CURVE ( 'NONE', #358, #4623, #103778, .T. ) ;
#96640=EDGE_LOOP ( 'NONE', ( #114453, #62973, #35431, #123815 ) ) ;
#96641=VERTEX_POINT ( 'NONE', #17503 ) ;
#96642=DIRECTION ( 'NONE',  ( -0.6830127018922181881, 0.6830127018922202975, -0.2588190451025214056 ) ) ;
#96643=ADVANCED_FACE ( 'NONE', ( #60332 ), #116098, .F. ) ;
#96644=LINE ( 'NONE', #121289, #56939 ) ;
#96645=CARTESIAN_POINT ( 'NONE',  ( -6.498163485139524909, -17.24070752338410628, 8.407044977365240257 ) ) ;
#96646=ORIENTED_EDGE ( 'NONE', *, *, #4882, .F. ) ;
#96647=DIRECTION ( 'NONE',  ( -0.7071067811865486830, 0.7071067811865464625, 0.000000000000000000 ) ) ;
#96648=DIRECTION ( 'NONE',  ( 0.6830127018922181881, 0.6830127018922202975, -0.2588190451025214056 ) ) ;
#96649=ORIENTED_EDGE ( 'NONE', *, *, #14102, .F. ) ;
#96652=CARTESIAN_POINT ( 'NONE',  ( -16.49999999999988987, -12.08601207473291872, -10.46905243149090836 ) ) ;
#96654=EDGE_CURVE ( 'NONE', #42509, #94617, #91518, .T. ) ;
#96655=CARTESIAN_POINT ( 'NONE',  ( -34.42500000000001137, 21.72500000000000142, 4.000000000000000000 ) ) ;
#96656=VERTEX_POINT ( 'NONE', #3057 ) ;
#96657=ORIENTED_EDGE ( 'NONE', *, *, #127022, .T. ) ;
#96658=VECTOR ( 'NONE', #74652, 1000.000000000000000 ) ;
#96661=DIRECTION ( 'NONE',  ( -0.6830127018922181881, 0.6830127018922202975, -0.2588190451025214056 ) ) ;
#96662=EDGE_CURVE ( 'NONE', #114524, #100040, #124844, .T. ) ;
#96663=LINE ( 'NONE', #117705, #47830 ) ;
#96664=DIRECTION ( 'NONE',  ( -0.7071067811865486830, -0.7071067811865464625, -0.000000000000000000 ) ) ;
#96665=VERTEX_POINT ( 'NONE', #138590 ) ;
#96666=EDGE_LOOP ( 'NONE', ( #108679, #38344, #80272, #36854, #136806, #126586 ) ) ;
#96668=LINE ( 'NONE', #41613, #28314 ) ;
#96669=ORIENTED_EDGE ( 'NONE', *, *, #28965, .F. ) ;
#96670=EDGE_CURVE ( 'NONE', #8586, #141224, #58941, .T. ) ;
#96671=VERTEX_POINT ( 'NONE', #5171 ) ;
#96674=DIRECTION ( 'NONE',  ( -0.7071067811865487940, 0.7071067811865463515, 0.000000000000000000 ) ) ;
#96676=ADVANCED_FACE ( 'NONE', ( #37119 ), #92927, .F. ) ;
#96677=FACE_OUTER_BOUND ( 'NONE', #109593, .T. ) ;
#96678=FACE_OUTER_BOUND ( 'NONE', #44203, .T. ) ;
#96679=VECTOR ( 'NONE', #120650, 1000.000000000000227 ) ;
#96680=EDGE_CURVE ( 'NONE', #18415, #37390, #61758, .T. ) ;
#96681=LINE ( 'NONE', #75003, #44299 ) ;
#96682=VECTOR ( 'NONE', #129509, 1000.000000000000000 ) ;
#96683=FACE_BOUND ( 'NONE', #29681, .T. ) ;
#96684=CARTESIAN_POINT ( 'NONE',  ( 39.29177708983023365, -15.74070752338412760, 19.73771281079106998 ) ) ;
#96687=CARTESIAN_POINT ( 'NONE',  ( -7.499999999999947597, -8.568876922607733704, 4.000000000000000000 ) ) ;
#96689=VECTOR ( 'NONE', #119523, 999.9999999999998863 ) ;
#96692=ORIENTED_EDGE ( 'NONE', *, *, #40297, .F. ) ;
#96693=ORIENTED_EDGE ( 'NONE', *, *, #138688, .T. ) ;
#96696=EDGE_CURVE ( 'NONE', #123294, #47726, #25519, .T. ) ;
#96697=DIRECTION ( 'NONE',  ( -0.000000000000000000, 0.000000000000000000, 1.000000000000000000 ) ) ;
#96699=CARTESIAN_POINT ( 'NONE',  ( -28.82816939922332011, 3.759292476615681888, 4.000000000000000000 ) ) ;
#96701=DIRECTION ( 'NONE',  ( 4.681814790819592407E-17, 0.3543493200069153248, 0.9351131265310292928 ) ) ;
#96702=CARTESIAN_POINT ( 'NONE',  ( -10.00193056682090997, -22.22500000000000142, 4.500000000000000888 ) ) ;
#96703=DIRECTION ( 'NONE',  ( 0.7071067811865487940, 0.7071067811865463515, 0.000000000000000000 ) ) ;
#96704=PLANE ( 'NONE',  #34305 ) ;
#96705=DIRECTION ( 'NONE',  ( -0.7071067811865486830, 0.7071067811865464625, 0.000000000000000000 ) ) ;
#96706=CARTESIAN_POINT ( 'NONE',  ( 20.99451991528748707, 28.92564299267952777, 4.000000000000000000 ) ) ;
#96707=CARTESIAN_POINT ( 'NONE',  ( 16.82816939922341248, -11.24070752338416490, 4.000000000000000000 ) ) ;
#96708=EDGE_LOOP ( 'NONE', ( #18598, #60158, #101093, #116880 ) ) ;
#96709=CARTESIAN_POINT ( 'NONE',  ( 48.18398860626899705, 28.73617430169820608, 5.000000000000000000 ) ) ;
#96711=LINE ( 'NONE', #7583, #98166 ) ;
#96713=ORIENTED_EDGE ( 'NONE', *, *, #142032, .T. ) ;
#96715=ORIENTED_EDGE ( 'NONE', *, *, #99424, .T. ) ;
#96719=ORIENTED_EDGE ( 'NONE', *, *, #46400, .F. ) ;
#96720=CARTESIAN_POINT ( 'NONE',  ( -51.29974487139158867, -27.71228299555242103, 4.000000000000000000 ) ) ;
#96721=( BOUNDED_CURVE ( )  B_SPLINE_CURVE ( 3, ( #85928, #64191, #106222, #6896 ),
 .UNSPECIFIED., .F., .T. ) 
 B_SPLINE_CURVE_WITH_KNOTS ( ( 4, 4 ),
 ( 1.248621635838844890, 1.295595743666721811 ),
 .UNSPECIFIED. ) 
 CURVE ( )  GEOMETRIC_REPRESENTATION_ITEM ( )  RATIONAL_B_SPLINE_CURVE ( ( 1.000000000000000000, 0.9998161278856747547, 0.9998161278856747547, 1.000000000000000000 ) ) 
 REPRESENTATION_ITEM ( '' )  );
#96724=ORIENTED_EDGE ( 'NONE', *, *, #64349, .F. ) ;
#96725=CARTESIAN_POINT ( 'NONE',  ( 18.40295003975137433, -2.759949774800250388, 4.658785122533355860 ) ) ;
#96726=ORIENTED_EDGE ( 'NONE', *, *, #116712, .T. ) ;
#96727=CYLINDRICAL_SURFACE ( 'NONE', #35932, 0.5000000000000004441 ) ;
#96729=ORIENTED_EDGE ( 'NONE', *, *, #93346, .T. ) ;
#96730=EDGE_LOOP ( 'NONE', ( #138474, #122290, #63934, #64498 ) ) ;
#96732=CARTESIAN_POINT ( 'NONE',  ( 12.48921356237309155, -27.52281430457064104, 5.000000000000000000 ) ) ;
#96734=CARTESIAN_POINT ( 'NONE',  ( -29.99451991528749417, 28.92564299267958816, 4.000000000000000000 ) ) ;
#96735=VERTEX_POINT ( 'NONE', #132559 ) ;
#96736=EDGE_CURVE ( 'NONE', #137044, #118417, #10700, .T. ) ;
#96738=ORIENTED_EDGE ( 'NONE', *, *, #112450, .T. ) ;
#96741=ORIENTED_EDGE ( 'NONE', *, *, #47699, .T. ) ;
#96742=LINE ( 'NONE', #86647, #37911 ) ;
#96743=CARTESIAN_POINT ( 'NONE',  ( -2.999999999999976463, -19.22509904557637128, 1.855685503482171983 ) ) ;
#96744=CARTESIAN_POINT ( 'NONE',  ( -6.280019679894003559, 0.7592924766157138627, 14.27032725228007415 ) ) ;
#96745=CARTESIAN_POINT ( 'NONE',  ( 15.18398860626900237, 28.73617430169797871, 5.000000000000000000 ) ) ;
#96748=EDGE_CURVE ( 'NONE', #136089, #101203, #110725, .T. ) ;
#96750=LINE ( 'NONE', #51161, #16443 ) ;
#96751=VERTEX_POINT ( 'NONE', #554 ) ;
#96752=CARTESIAN_POINT ( 'NONE',  ( 48.29974487139158867, -27.71228299555239971, 4.000000000000000000 ) ) ;
#96755=LINE ( 'NONE', #143157, #11298 ) ;
#96756=VECTOR ( 'NONE', #101553, 1000.000000000000000 ) ;
#96757=LINE ( 'NONE', #21394, #49001 ) ;
#96758=VERTEX_POINT ( 'NONE', #65145 ) ;
#96759=ORIENTED_EDGE ( 'NONE', *, *, #130415, .F. ) ;
#96760=PLANE ( 'NONE',  #58600 ) ;
#96761=DIRECTION ( 'NONE',  ( 0.6830127018922181881, 0.6830127018922202975, -0.2588190451025214056 ) ) ;
#96764=CARTESIAN_POINT ( 'NONE',  ( 34.42499999999998295, 22.22500000000000142, 5.000000000000000000 ) ) ;
#96765=LINE ( 'NONE', #141020, #62313 ) ;
#96766=CARTESIAN_POINT ( 'NONE',  ( 28.00193056682079273, -22.22500000000000142, 4.500000000000000888 ) ) ;
#96767=CARTESIAN_POINT ( 'NONE',  ( 8.999999999999937828, -9.412538124160663600, 4.000000000000000000 ) ) ;
#96768=ORIENTED_EDGE ( 'NONE', *, *, #61772, .F. ) ;
#96769=CARTESIAN_POINT ( 'NONE',  ( 6.328169399223485314, 2.259292476615697876, 4.000000000000000000 ) ) ;
#96770=EDGE_CURVE ( 'NONE', #76705, #39505, #89038, .T. ) ;
#96771=ORIENTED_EDGE ( 'NONE', *, *, #96489, .F. ) ;
#96772=LINE ( 'NONE', #85946, #80261 ) ;
#96774=VERTEX_POINT ( 'NONE', #74041 ) ;
#96775=AXIS2_PLACEMENT_3D ( 'NONE', #86978, #11522, #22404 ) ;
#96777=DIRECTION ( 'NONE',  ( -0.6830127018922180770, -0.6830127018922204085, -0.2588190451025213501 ) ) ;
#96778=PLANE ( 'NONE',  #30371 ) ;
#96779=ORIENTED_EDGE ( 'NONE', *, *, #30153, .F. ) ;
#96780=VECTOR ( 'NONE', #30782, 1000.000000000000000 ) ;
#96781=DIRECTION ( 'NONE',  ( 1.000000000000000000, 0.000000000000000000, 0.000000000000000000 ) ) ;
#96782=CARTESIAN_POINT ( 'NONE',  ( -60.18398860626900415, 28.73617430169829490, 5.000000000000000000 ) ) ;
#96784=EDGE_CURVE ( 'NONE', #29835, #66621, #44561, .T. ) ;
#96785=EDGE_CURVE ( 'NONE', #107216, #74602, #129124, .T. ) ;
#96786=EDGE_CURVE ( 'NONE', #77009, #102711, #84909, .T. ) ;
#96788=VERTEX_POINT ( 'NONE', #99141 ) ;
#96790=CARTESIAN_POINT ( 'NONE',  ( -14.99999999999989519, -2.904428200921318481, -6.989807076074906256 ) ) ;
#96791=VECTOR ( 'NONE', #128147, 1000.000000000000227 ) ;
#96792=VECTOR ( 'NONE', #126003, 1000.000000000000000 ) ;
#96793=CARTESIAN_POINT ( 'NONE',  ( 32.99999999999977263, 18.08204922493375832, 0.9627537363044108565 ) ) ;
#96796=ADVANCED_FACE ( 'NONE', ( #76737 ), #11408, .F. ) ;
#96797=LINE ( 'NONE', #8360, #4552 ) ;
#96798=DIRECTION ( 'NONE',  ( 0.7071067811865487940, 0.7071067811865463515, 0.000000000000000000 ) ) ;
#96799=ORIENTED_EDGE ( 'NONE', *, *, #137261, .F. ) ;
#96800=EDGE_CURVE ( 'NONE', #115116, #90399, #117512, .T. ) ;
#96802=EDGE_CURVE ( 'NONE', #12209, #14811, #106632, .T. ) ;
#96803=DIRECTION ( 'NONE',  ( -0.7071067811865487940, 0.7071067811865463515, 0.000000000000000000 ) ) ;
#96806=ADVANCED_FACE ( 'NONE', ( #20880 ), #101313, .F. ) ;
#96807=ORIENTED_EDGE ( 'NONE', *, *, #19455, .T. ) ;
#96808=DIRECTION ( 'NONE',  ( 0.7071067811865487940, -0.7071067811865463515, 0.000000000000000000 ) ) ;
#96809=EDGE_CURVE ( 'NONE', #70950, #4634, #14300, .T. ) ;
#96810=EDGE_LOOP ( 'NONE', ( #132319, #72849, #118167 ) ) ;
#96812=CARTESIAN_POINT ( 'NONE',  ( -39.29974487139159578, -27.71228299555233576, 4.000000000000000000 ) ) ;
#96813=CARTESIAN_POINT ( 'NONE',  ( 60.48921356237309510, -27.52281430457097500, 5.000000000000000000 ) ) ;
#96814=VECTOR ( 'NONE', #97540, 1000.000000000000000 ) ;
#96815=ORIENTED_EDGE ( 'NONE', *, *, #98549, .T. ) ;
#96816=CARTESIAN_POINT ( 'NONE',  ( 6.722814304570563948, -21.72499999999999432, 5.000000000000000000 ) ) ;
#96817=AXIS2_PLACEMENT_3D ( 'NONE', #139464, #128553, #63328 ) ;
#96818=EDGE_CURVE ( 'NONE', #97623, #131861, #36760, .T. ) ;
#96819=DIRECTION ( 'NONE',  ( -0.000000000000000000, 0.000000000000000000, 1.000000000000000000 ) ) ;
#96820=AXIS2_PLACEMENT_3D ( 'NONE', #78965, #23083, #34019 ) ;
#96821=CARTESIAN_POINT ( 'NONE',  ( 3.812461875839446623, -22.22500000000000142, 4.000000000000000000 ) ) ;
#96823=CARTESIAN_POINT ( 'NONE',  ( -30.48921356237309510, -27.52281430457076894, 5.000000000000000000 ) ) ;
#96824=VERTEX_POINT ( 'NONE', #3402 ) ;
#96825=DIRECTION ( 'NONE',  ( 0.6830127018922180770, -0.6830127018922204085, -0.2588190451025213501 ) ) ;
#96826=PLANE ( 'NONE',  #105509 ) ;
#96827=LINE ( 'NONE', #64978, #21658 ) ;
#96828=EDGE_CURVE ( 'NONE', #21420, #16508, #1261, .T. ) ;
#96829=DIRECTION ( 'NONE',  ( -0.7071067811865486830, -0.7071067811865464625, 0.000000000000000000 ) ) ;
#96830=VERTEX_POINT ( 'NONE', #113606 ) ;
#96833=VERTEX_POINT ( 'NONE', #13563 ) ;
#96834=FACE_OUTER_BOUND ( 'NONE', #66217, .T. ) ;
#96836=CARTESIAN_POINT ( 'NONE',  ( 11.81601139373100651, 28.73617430169779041, 5.000000000000000000 ) ) ;
#96838=VERTEX_POINT ( 'NONE', #136795 ) ;
#96839=VECTOR ( 'NONE', #50757, 1000.000000000000000 ) ;
#96840=CARTESIAN_POINT ( 'NONE',  ( 22.98012225071438408, -17.24070752338410628, 20.23474786156474892 ) ) ;
#96843=EDGE_CURVE ( 'NONE', #73204, #56643, #83486, .T. ) ;
#96845=CARTESIAN_POINT ( 'NONE',  ( -9.489213562373095101, -27.52281430457062328, 5.000000000000000000 ) ) ;
#96846=ADVANCED_FACE ( 'NONE', ( #103432 ), #47693, .F. ) ;
#96847=DIRECTION ( 'NONE',  ( -0.7071067811865486830, -0.7071067811865464625, 0.000000000000000000 ) ) ;
#96848=CARTESIAN_POINT ( 'NONE',  ( -29.29298673570674794, -21.74070752338405299, 4.999753212805210012 ) ) ;
#96849=EDGE_CURVE ( 'NONE', #12864, #32966, #125936, .T. ) ;
#96851=ORIENTED_EDGE ( 'NONE', *, *, #120799, .F. ) ;
#96852=FACE_BOUND ( 'NONE', #101465, .T. ) ;
#96853=DIRECTION ( 'NONE',  ( 0.7071067811865486830, -0.7071067811865464625, -0.000000000000000000 ) ) ;
#96858=LINE ( 'NONE', #53392, #41926 ) ;
#96859=ORIENTED_EDGE ( 'NONE', *, *, #30710, .F. ) ;
#96860=ORIENTED_EDGE ( 'NONE', *, *, #105798, .F. ) ;
#96861=ORIENTED_EDGE ( 'NONE', *, *, #109373, .F. ) ;
#96862=ADVANCED_FACE ( 'NONE', ( #81010 ), #125213, .F. ) ;
#96863=ORIENTED_EDGE ( 'NONE', *, *, #86610, .T. ) ;
#96865=CARTESIAN_POINT ( 'NONE',  ( -72.18398860626899705, 28.73617430169837661, 5.000000000000000000 ) ) ;
#96866=DIRECTION ( 'NONE',  ( -0.7071067811865487940, 0.7071067811865463515, -0.000000000000000000 ) ) ;
#96869=CARTESIAN_POINT ( 'NONE',  ( 25.49999999999982947, -7.912538124160678699, 4.000000000000000000 ) ) ;
#96870=VECTOR ( 'NONE', #843, 1000.000000000000227 ) ;
#96871=EDGE_CURVE ( 'NONE', #64975, #134832, #37507, .T. ) ;
#96873=CARTESIAN_POINT ( 'NONE',  ( -5.816011393731002066, 28.73617430169783304, 5.000000000000000000 ) ) ;
#96874=VECTOR ( 'NONE', #114381, 1000.000000000000000 ) ;
#96875=VECTOR ( 'NONE', #80943, 1000.000000000000000 ) ;
#96876=LINE ( 'NONE', #54867, #39851 ) ;
#96877=ORIENTED_EDGE ( 'NONE', *, *, #97822, .F. ) ;
#96878=CARTESIAN_POINT ( 'NONE',  ( 38.91508676806214595, -12.74070752338415247, 18.74364270924363396 ) ) ;
#96879=PLANE ( 'NONE',  #67445 ) ;
#96880=AXIS2_PLACEMENT_3D ( 'NONE', #116169, #105286, #5940 ) ;
#96881=VERTEX_POINT ( 'NONE', #4076 ) ;
#96882=CARTESIAN_POINT ( 'NONE',  ( -24.99033360189226372, 3.759292476615678336, 4.478963035907990609 ) ) ;
#96883=ADVANCED_FACE ( 'NONE', ( #92554 ), #91185, .T. ) ;
#96884=EDGE_LOOP ( 'NONE', ( #123143, #18906, #70452, #92452 ) ) ;
#96885=VERTEX_POINT ( 'NONE', #100614 ) ;
#96886=ORIENTED_EDGE ( 'NONE', *, *, #77730, .F. ) ;
#96887=EDGE_CURVE ( 'NONE', #45259, #129569, #35384, .T. ) ;
#96889=AXIS2_PLACEMENT_3D ( 'NONE', #62366, #139221, #6483 ) ;
#96892=AXIS2_PLACEMENT_3D ( 'NONE', #52004, #49879, #94061 ) ;
#96893=CARTESIAN_POINT ( 'NONE',  ( -34.17183060077622514, -5.240707523384232402, 4.000000000000000000 ) ) ;
#96894=ADVANCED_FACE ( 'NONE', ( #78875 ), #123083, .F. ) ;
#96896=CARTESIAN_POINT ( 'NONE',  ( 19.61351471301484395, 9.118430946277904070, 4.525620927308371400 ) ) ;
#96897=DIRECTION ( 'NONE',  ( 0.7071067811865487940, 0.7071067811865463515, -0.000000000000000000 ) ) ;
#96898=EDGE_LOOP ( 'NONE', ( #112410, #122542, #68635, #3878 ) ) ;
#96899=DIRECTION ( 'NONE',  ( -0.7071067811865486830, -0.7071067811865464625, 0.000000000000000000 ) ) ;
#96900=DIRECTION ( 'NONE',  ( 0.7071067811865487940, 0.7071067811865463515, 0.000000000000000000 ) ) ;
#96901=EDGE_CURVE ( 'NONE', #65140, #105391, #46259, .T. ) ;
#96902=FACE_OUTER_BOUND ( 'NONE', #74054, .T. ) ;
#96906=EDGE_CURVE ( 'NONE', #121985, #88187, #36080, .T. ) ;
#96907=ORIENTED_EDGE ( 'NONE', *, *, #20668, .F. ) ;
#96908=ORIENTED_EDGE ( 'NONE', *, *, #22179, .F. ) ;
#96909=ORIENTED_EDGE ( 'NONE', *, *, #42969, .T. ) ;
#96911=AXIS2_PLACEMENT_3D ( 'NONE', #120320, #97906, #31930 ) ;
#96912=ORIENTED_EDGE ( 'NONE', *, *, #112028, .F. ) ;
#96913=VECTOR ( 'NONE', #8727, 1000.000000000000227 ) ;
#96914=VECTOR ( 'NONE', #28172, 1000.000000000000000 ) ;
#96915=DIRECTION ( 'NONE',  ( 1.000000000000000000, 0.000000000000000000, 0.000000000000000000 ) ) ;
#96916=DIRECTION ( 'NONE',  ( 0.7071067811865487940, 0.7071067811865463515, 0.000000000000000000 ) ) ;
#96917=VECTOR ( 'NONE', #70119, 1000.000000000000227 ) ;
#96918=CARTESIAN_POINT ( 'NONE',  ( -36.18398860626899705, 28.73617430169812437, 5.000000000000000000 ) ) ;
#96920=ORIENTED_EDGE ( 'NONE', *, *, #95368, .T. ) ;
#96922=ORIENTED_EDGE ( 'NONE', *, *, #117154, .F. ) ;
#96924=VECTOR ( 'NONE', #91095, 1000.000000000000000 ) ;
#96926=LINE ( 'NONE', #76674, #48388 ) ;
#96928=VERTEX_POINT ( 'NONE', #15681 ) ;
#96929=EDGE_LOOP ( 'NONE', ( #69831, #8555, #51723, #29138, #26571 ) ) ;
#96930=ORIENTED_EDGE ( 'NONE', *, *, #55216, .F. ) ;
#96931=DIRECTION ( 'NONE',  ( -0.000000000000000000, 0.000000000000000000, 1.000000000000000000 ) ) ;
#96932=LINE ( 'NONE', #118715, #141299 ) ;
#96933=VECTOR ( 'NONE', #140992, 999.9999999999998863 ) ;
#96934=FACE_OUTER_BOUND ( 'NONE', #125120, .T. ) ;
#96936=DIRECTION ( 'NONE',  ( 0.7071067811865487940, 0.7071067811865463515, 0.000000000000000000 ) ) ;
#96937=CARTESIAN_POINT ( 'NONE',  ( 11.99999999999991296, -19.06887692260762179, 4.000000000000000000 ) ) ;
#96939=LINE ( 'NONE', #72426, #115796 ) ;
#96941=VERTEX_POINT ( 'NONE', #93294 ) ;
#96942=DIRECTION ( 'NONE',  ( -0.7071067811865486830, -0.7071067811865464625, -0.000000000000000000 ) ) ;
#96943=CARTESIAN_POINT ( 'NONE',  ( -21.71238017851530344, 8.518175273744141407, 4.330735335516833651 ) ) ;
#96944=ORIENTED_EDGE ( 'NONE', *, *, #91628, .F. ) ;
#96945=LINE ( 'NONE', #129608, #113094 ) ;
#96947=ORIENTED_EDGE ( 'NONE', *, *, #104560, .F. ) ;
#96948=PLANE ( 'NONE',  #139471 ) ;
#96950=DIRECTION ( 'NONE',  ( -0.6830127018922181881, 0.6830127018922202975, -0.2588190451025214056 ) ) ;
#96951=ORIENTED_EDGE ( 'NONE', *, *, #45348, .T. ) ;
#96952=LINE ( 'NONE', #29585, #46684 ) ;
#96954=ORIENTED_EDGE ( 'NONE', *, *, #10153, .F. ) ;
#96958=CARTESIAN_POINT ( 'NONE',  ( 0.000000000000000000, 7.007997736742450634, -8.085015511992116544 ) ) ;
#96959=DIRECTION ( 'NONE',  ( -0.7071067811865486830, -0.7071067811865464625, 0.000000000000000000 ) ) ;
#96961=PLANE ( 'NONE',  #127830 ) ;
#96963=EDGE_CURVE ( 'NONE', #74781, #91404, #5547, .T. ) ;
#96964=LINE ( 'NONE', #74561, #66968 ) ;
#96967=FACE_OUTER_BOUND ( 'NONE', #45363, .T. ) ;
#96968=FACE_OUTER_BOUND ( 'NONE', #78977, .T. ) ;
#96969=ADVANCED_FACE ( 'NONE', ( #28767 ), #140362, .F. ) ;
#96970=EDGE_LOOP ( 'NONE', ( #24373, #45458, #31485, #65783 ) ) ;
#96971=ORIENTED_EDGE ( 'NONE', *, *, #130448, .T. ) ;
#96973=ORIENTED_EDGE ( 'NONE', *, *, #81629, .F. ) ;
#96975=LINE ( 'NONE', #141983, #73518 ) ;
#96976=DIRECTION ( 'NONE',  ( -0.3543493200069162685, -0.000000000000000000, -0.9351131265310288487 ) ) ;
#96979=AXIS2_PLACEMENT_3D ( 'NONE', #73575, #117745, #85145 ) ;
#96980=VECTOR ( 'NONE', #16179, 1000.000000000000000 ) ;
#96981=AXIS2_PLACEMENT_3D ( 'NONE', #116308, #127174, #72862 ) ;
#96982=FACE_OUTER_BOUND ( 'NONE', #81277, .T. ) ;
#96983=AXIS2_PLACEMENT_3D ( 'NONE', #50735, #117380, #39148 ) ;
#96984=ADVANCED_FACE ( 'NONE', ( #26609 ), #128773, .F. ) ;
#96986=EDGE_CURVE ( 'NONE', #101708, #138040, #38916, .T. ) ;
#96987=CARTESIAN_POINT ( 'NONE',  ( 42.18398860626899705, 28.73617430169816700, 5.000000000000000000 ) ) ;
#96991=DIRECTION ( 'NONE',  ( -0.3543493200069162685, -0.000000000000000000, -0.9351131265310288487 ) ) ;
#96992=VECTOR ( 'NONE', #129797, 999.9999999999998863 ) ;
#96993=EDGE_CURVE ( 'NONE', #20187, #68937, #16414, .T. ) ;
#96995=EDGE_LOOP ( 'NONE', ( #47751, #114575, #135129, #13459 ) ) ;
#96996=VERTEX_POINT ( 'NONE', #6947 ) ;
#96997=ORIENTED_EDGE ( 'NONE', *, *, #132572, .T. ) ;
#96999=ORIENTED_EDGE ( 'NONE', *, *, #47476, .T. ) ;
#97001=VECTOR ( 'NONE', #100039, 1000.000000000000000 ) ;
#97002=LINE ( 'NONE', #86898, #47819 ) ;
#97003=ORIENTED_EDGE ( 'NONE', *, *, #22569, .T. ) ;
#97005=PLANE ( 'NONE',  #41983 ) ;
#97006=AXIS2_PLACEMENT_3D ( 'NONE', #74949, #41561, #30723 ) ;
#97009=CARTESIAN_POINT ( 'NONE',  ( -5.292893218813415679, 14.25929247661557575, 5.000000000000000000 ) ) ;
#97011=EDGE_CURVE ( 'NONE', #80483, #72728, #83138, .T. ) ;
#97012=DIRECTION ( 'NONE',  ( -0.7071067811865486830, -0.7071067811865464625, -0.000000000000000000 ) ) ;
#97013=AXIS2_PLACEMENT_3D ( 'NONE', #69251, #135919, #101137 ) ;
#97014=DIRECTION ( 'NONE',  ( -0.7071067811865486830, -0.7071067811865464625, 0.000000000000000000 ) ) ;
#97016=VECTOR ( 'NONE', #113031, 1000.000000000000000 ) ;
#97017=ORIENTED_EDGE ( 'NONE', *, *, #90193, .T. ) ;
#97018=VERTEX_POINT ( 'NONE', #85255 ) ;
#97019=ORIENTED_EDGE ( 'NONE', *, *, #18565, .F. ) ;
#97020=CARTESIAN_POINT ( 'NONE',  ( 28.49999999999981171, 22.22500000000000142, 4.362957392718781691 ) ) ;
#97021=DIRECTION ( 'NONE',  ( -0.6830127018922180770, -0.6830127018922204085, -0.2588190451025213501 ) ) ;
#97023=VECTOR ( 'NONE', #73671, 999.9999999999998863 ) ;
#97026=ADVANCED_FACE ( 'NONE', ( #94695 ), #17167, .F. ) ;
#97027=ORIENTED_EDGE ( 'NONE', *, *, #26787, .T. ) ;
#97030=EDGE_CURVE ( 'NONE', #128836, #10662, #40372, .T. ) ;
#97031=ORIENTED_EDGE ( 'NONE', *, *, #125024, .F. ) ;
#97032=ORIENTED_EDGE ( 'NONE', *, *, #30398, .F. ) ;
#97033=VECTOR ( 'NONE', #35693, 1000.000000000000000 ) ;
#97034=CARTESIAN_POINT ( 'NONE',  ( 0.000000000000000000, 0.000000000000000000, 5.000000000000000000 ) ) ;
#97035=DIRECTION ( 'NONE',  ( 0.3543493200069162685, -0.000000000000000000, -0.9351131265310288487 ) ) ;
#97036=ORIENTED_EDGE ( 'NONE', *, *, #86620, .F. ) ;
#97038=EDGE_CURVE ( 'NONE', #57193, #15218, #61430, .T. ) ;
#97039=CARTESIAN_POINT ( 'NONE',  ( 11.99999999999992006, 10.93112307739207267, 4.000000000000000000 ) ) ;
#97040=CARTESIAN_POINT ( 'NONE',  ( -29.99999999999979394, 12.83542986846994793, -1.025386466790300544 ) ) ;
#97041=DIRECTION ( 'NONE',  ( -0.7071067811865486830, -0.7071067811865464625, 0.000000000000000000 ) ) ;
#97043=VERTEX_POINT ( 'NONE', #138958 ) ;
#97046=EDGE_CURVE ( 'NONE', #9024, #4889, #84575, .T. ) ;
#97047=ORIENTED_EDGE ( 'NONE', *, *, #27004, .F. ) ;
#97049=ORIENTED_EDGE ( 'NONE', *, *, #61707, .F. ) ;
#97051=ORIENTED_EDGE ( 'NONE', *, *, #142023, .T. ) ;
#97052=ORIENTED_EDGE ( 'NONE', *, *, #103897, .T. ) ;
#97055=FACE_OUTER_BOUND ( 'NONE', #127919, .T. ) ;
#97056=CARTESIAN_POINT ( 'NONE',  ( -4.828169399223493308, -5.240707523384230626, 4.000000000000000000 ) ) ;
#97058=DIRECTION ( 'NONE',  ( 0.3543493200069162685, -0.000000000000000000, -0.9351131265310288487 ) ) ;
#97059=DIRECTION ( 'NONE',  ( -0.000000000000000000, 0.3543493200069153248, 0.9351131265310292928 ) ) ;
#97061=FACE_OUTER_BOUND ( 'NONE', #125168, .T. ) ;
#97062=CARTESIAN_POINT ( 'NONE',  ( 5.999999999999956479, 12.25461709320621928, -10.07315571508695839 ) ) ;
#97063=EDGE_CURVE ( 'NONE', #43532, #37108, #76564, .T. ) ;
#97064=PLANE ( 'NONE',  #62180 ) ;
#97065=CARTESIAN_POINT ( 'NONE',  ( 31.49999999999978684, 10.94296225409029510, -9.576120664313185316 ) ) ;
#97066=EDGE_CURVE ( 'NONE', #25651, #39180, #41775, .T. ) ;
#97067=ORIENTED_EDGE ( 'NONE', *, *, #4100, .T. ) ;
#97068=EDGE_LOOP ( 'NONE', ( #119558, #37722, #28493, #42769 ) ) ;
#97070=ORIENTED_EDGE ( 'NONE', *, *, #109907, .F. ) ;
#97071=VERTEX_POINT ( 'NONE', #119308 ) ;
#97072=CARTESIAN_POINT ( 'NONE',  ( -36.18398860626899705, 28.73617430169812437, 5.000000000000000000 ) ) ;
#97074=VECTOR ( 'NONE', #122264, 1000.000000000000000 ) ;
#97075=EDGE_LOOP ( 'NONE', ( #113097, #116742, #99207, #10536 ) ) ;
#97076=AXIS2_PLACEMENT_3D ( 'NONE', #933, #17354, #89393 ) ;
#97077=VECTOR ( 'NONE', #50558, 999.9999999999998863 ) ;
#97078=ORIENTED_EDGE ( 'NONE', *, *, #36289, .F. ) ;
#97079=DIRECTION ( 'NONE',  ( -0.7071067811865486830, -0.7071067811865464625, 0.000000000000000000 ) ) ;
#97081=EDGE_CURVE ( 'NONE', #129291, #42695, #43921, .T. ) ;
#97083=DIRECTION ( 'NONE',  ( -0.6830127018922180770, -0.6830127018922204085, -0.2588190451025213501 ) ) ;
#97084=VERTEX_POINT ( 'NONE', #32330 ) ;
#97085=CARTESIAN_POINT ( 'NONE',  ( 21.18398860626899349, 28.73617430169802134, 5.000000000000000000 ) ) ;
#97086=AXIS2_PLACEMENT_3D ( 'NONE', #19441, #52766, #120884 ) ;
#97087=ORIENTED_EDGE ( 'NONE', *, *, #136436, .T. ) ;
#97089=LINE ( 'NONE', #120273, #70519 ) ;
#97091=VECTOR ( 'NONE', #93051, 1000.000000000000227 ) ;
#97094=DIRECTION ( 'NONE',  ( 0.7071067811865487940, -0.7071067811865463515, 0.000000000000000000 ) ) ;
#97097=EDGE_LOOP ( 'NONE', ( #124625, #74151, #116572, #116078 ) ) ;
#97098=ORIENTED_EDGE ( 'NONE', *, *, #29222, .F. ) ;
#97100=EDGE_LOOP ( 'NONE', ( #51101, #112818, #124731, #93001 ) ) ;
#97103=PLANE ( 'NONE',  #139570 ) ;
#97104=DIRECTION ( 'NONE',  ( -0.3543493200069162685, -0.000000000000000000, -0.9351131265310288487 ) ) ;
#97106=ORIENTED_EDGE ( 'NONE', *, *, #25554, .T. ) ;
#97107=CARTESIAN_POINT ( 'NONE',  ( 6.489213562373093325, -27.52281430457059841, 5.000000000000000000 ) ) ;
#97109=CARTESIAN_POINT ( 'NONE',  ( 30.70710678118633297, 20.25929247661551713, 5.000000000000000000 ) ) ;
#97110=FACE_OUTER_BOUND ( 'NONE', #93747, .T. ) ;
#97112=DIRECTION ( 'NONE',  ( -0.7071067811865486830, -0.7071067811865464625, 0.000000000000000000 ) ) ;
#97113=VECTOR ( 'NONE', #119150, 1000.000000000000227 ) ;
#97114=PLANE ( 'NONE',  #3022 ) ;
#97116=VERTEX_POINT ( 'NONE', #118605 ) ;
#97118=DIRECTION ( 'NONE',  ( -0.7071067811865486830, -0.7071067811865464625, 0.000000000000000000 ) ) ;
#97119=ORIENTED_EDGE ( 'NONE', *, *, #30942, .T. ) ;
#97120=ORIENTED_EDGE ( 'NONE', *, *, #139423, .T. ) ;
#97121=VECTOR ( 'NONE', #58111, 1000.000000000000000 ) ;
#97122=DIRECTION ( 'NONE',  ( -0.000000000000000000, -0.3543493200069152693, 0.9351131265310292928 ) ) ;
#97123=VECTOR ( 'NONE', #103255, 1000.000000000000000 ) ;
#97124=DIRECTION ( 'NONE',  ( 1.000000000000000000, 0.000000000000000000, 0.000000000000000000 ) ) ;
#97125=ORIENTED_EDGE ( 'NONE', *, *, #64689, .F. ) ;
#97126=FACE_OUTER_BOUND ( 'NONE', #131843, .T. ) ;
#97127=CARTESIAN_POINT ( 'NONE',  ( -29.20710678118632586, -14.24070752338413648, 5.000000000000000000 ) ) ;
#97128=EDGE_CURVE ( 'NONE', #124871, #31809, #141066, .T. ) ;
#97131=CARTESIAN_POINT ( 'NONE',  ( -21.29974487139158512, -27.71228299555221142, 4.000000000000000000 ) ) ;
#97132=EDGE_CURVE ( 'NONE', #95686, #18692, #132385, .T. ) ;
#97134=CARTESIAN_POINT ( 'NONE',  ( 12.06011071044012439, -9.740707523384180888, 10.89222023123378058 ) ) ;
#97136=PLANE ( 'NONE',  #66866 ) ;
#97137=CARTESIAN_POINT ( 'NONE',  ( -24.70710678118637560, 14.25929247661557753, 5.000000000000000000 ) ) ;
#97139=DIRECTION ( 'NONE',  ( -0.7071067811865487940, 0.7071067811865463515, -0.000000000000000000 ) ) ;
#97140=DIRECTION ( 'NONE',  ( -0.7071067811865487940, 0.7071067811865463515, 0.000000000000000000 ) ) ;
#97141=DIRECTION ( 'NONE',  ( -0.7071067811865486830, -0.7071067811865464625, -0.000000000000000000 ) ) ;
#97142=DIRECTION ( 'NONE',  ( -0.7071067811865486830, -0.7071067811865464625, -0.000000000000000000 ) ) ;
#97145=EDGE_CURVE ( 'NONE', #36373, #11113, #97563, .T. ) ;
#97146=VERTEX_POINT ( 'NONE', #31614 ) ;
#97149=ORIENTED_EDGE ( 'NONE', *, *, #78454, .F. ) ;
#97150=ORIENTED_EDGE ( 'NONE', *, *, #138670, .F. ) ;
#97151=VERTEX_POINT ( 'NONE', #96821 ) ;
#97152=CARTESIAN_POINT ( 'NONE',  ( 15.79076468313838433, 8.175634574663693144, 5.000000000000000000 ) ) ;
#97153=DIRECTION ( 'NONE',  ( -0.7071067811865486830, -0.7071067811865464625, -0.000000000000000000 ) ) ;
#97155=DIRECTION ( 'NONE',  ( 0.7071067811865487940, 0.7071067811865463515, 0.000000000000000000 ) ) ;
#97156=CARTESIAN_POINT ( 'NONE',  ( -30.32816939922332367, 11.25929247661560950, 4.000000000000000000 ) ) ;
#97157=EDGE_CURVE ( 'NONE', #6537, #140758, #8380, .T. ) ;
#97158=DIRECTION ( 'NONE',  ( -0.000000000000000000, -0.3543493200069152693, 0.9351131265310292928 ) ) ;
#97159=DIRECTION ( 'NONE',  ( -0.6830127018922180770, -0.6830127018922204085, -0.2588190451025213501 ) ) ;
#97161=ORIENTED_EDGE ( 'NONE', *, *, #79908, .T. ) ;
#97162=EDGE_CURVE ( 'NONE', #107216, #22385, #110563, .T. ) ;
#97164=LINE ( 'NONE', #63193, #24176 ) ;
#97165=LINE ( 'NONE', #121793, #128519 ) ;
#97166=PLANE ( 'NONE',  #72405 ) ;
#97167=DIRECTION ( 'NONE',  ( 0.7071067811865487940, 0.7071067811865463515, 0.000000000000000000 ) ) ;
#97169=EDGE_CURVE ( 'NONE', #57216, #31488, #86718, .T. ) ;
#97170=DIRECTION ( 'NONE',  ( -0.7071067811865487940, 0.7071067811865463515, 0.000000000000000000 ) ) ;
#97171=ORIENTED_EDGE ( 'NONE', *, *, #33163, .F. ) ;
#97172=ORIENTED_EDGE ( 'NONE', *, *, #32611, .F. ) ;
#97174=ORIENTED_EDGE ( 'NONE', *, *, #42781, .F. ) ;
#97176=LINE ( 'NONE', #10198, #40910 ) ;
#97177=ADVANCED_FACE ( 'NONE', ( #42512 ), #11242, .F. ) ;
#97178=CARTESIAN_POINT ( 'NONE',  ( 65.99451991528749772, 28.92564299267984396, 4.000000000000000000 ) ) ;
#97179=DIRECTION ( 'NONE',  ( -0.7071067811865486830, -0.7071067811865464625, 0.000000000000000000 ) ) ;
#97180=DIRECTION ( 'NONE',  ( -0.6830127018922180770, -0.6830127018922204085, -0.2588190451025214056 ) ) ;
#97181=DIRECTION ( 'NONE',  ( -0.3543493200069163240, -0.000000000000000000, 0.9351131265310288487 ) ) ;
#97182=VECTOR ( 'NONE', #79548, 1000.000000000000000 ) ;
#97184=ORIENTED_EDGE ( 'NONE', *, *, #82369, .F. ) ;
#97186=VECTOR ( 'NONE', #79989, 1000.000000000000000 ) ;
#97187=VERTEX_POINT ( 'NONE', #378 ) ;
#97188=EDGE_CURVE ( 'NONE', #47375, #98565, #44671, .T. ) ;
#97190=VECTOR ( 'NONE', #82698, 1000.000000000000000 ) ;
#97194=CARTESIAN_POINT ( 'NONE',  ( 33.48921356237309510, -27.52281430457078670, 5.000000000000000000 ) ) ;
#97195=VECTOR ( 'NONE', #136503, 1000.000000000000000 ) ;
#97196=DIRECTION ( 'NONE',  ( 0.7071067811865487940, -0.7071067811865463515, 0.000000000000000000 ) ) ;
#97197=ORIENTED_EDGE ( 'NONE', *, *, #130205, .F. ) ;
#97199=ORIENTED_EDGE ( 'NONE', *, *, #32023, .T. ) ;
#97200=CARTESIAN_POINT ( 'NONE',  ( -34.92500000000001137, -2.240707523384260824, 4.255531930566247567 ) ) ;
#97201=DIRECTION ( 'NONE',  ( 0.7071067811865487940, -0.7071067811865463515, 0.000000000000000000 ) ) ;
#97203=EDGE_CURVE ( 'NONE', #65062, #47033, #107721, .T. ) ;
#97204=PLANE ( 'NONE',  #129399 ) ;
#97205=VECTOR ( 'NONE', #11215, 1000.000000000000227 ) ;
#97206=EDGE_CURVE ( 'NONE', #43477, #104700, #129477, .T. ) ;
#97208=ORIENTED_EDGE ( 'NONE', *, *, #85383, .F. ) ;
#97210=ORIENTED_EDGE ( 'NONE', *, *, #129699, .T. ) ;
#97211=VERTEX_POINT ( 'NONE', #9843 ) ;
#97212=AXIS2_PLACEMENT_3D ( 'NONE', #77072, #21936, #30705 ) ;
#97213=ORIENTED_EDGE ( 'NONE', *, *, #130799, .F. ) ;
#97214=AXIS2_PLACEMENT_3D ( 'NONE', #82970, #105408, #128609 ) ;
#97215=PLANE ( 'NONE',  #42867 ) ;
#97216=DIRECTION ( 'NONE',  ( 0.6830127018922180770, -0.6830127018922204085, -0.2588190451025213501 ) ) ;
#97218=CARTESIAN_POINT ( 'NONE',  ( 13.17183060077638324, 6.759292476615645917, 4.000000000000000000 ) ) ;
#97220=DIRECTION ( 'NONE',  ( 0.7071067811865487940, 0.7071067811865463515, 0.000000000000000000 ) ) ;
#97221=VECTOR ( 'NONE', #71022, 1000.000000000000000 ) ;
#97222=FACE_OUTER_BOUND ( 'NONE', #83643, .T. ) ;
#97223=FACE_BOUND ( 'NONE', #100664, .T. ) ;
#97224=VERTEX_POINT ( 'NONE', #64240 ) ;
#97226=EDGE_CURVE ( 'NONE', #66880, #11497, #14118, .T. ) ;
#97227=VECTOR ( 'NONE', #26727, 1000.000000000000000 ) ;
#97229=DIRECTION ( 'NONE',  ( -0.7071067811865487940, 0.7071067811865463515, 0.000000000000000000 ) ) ;
#97230=VERTEX_POINT ( 'NONE', #47530 ) ;
#97232=ORIENTED_EDGE ( 'NONE', *, *, #60436, .T. ) ;
#97234=ORIENTED_EDGE ( 'NONE', *, *, #131184, .T. ) ;
#97235=PLANE ( 'NONE',  #77297 ) ;
#97236=VERTEX_POINT ( 'NONE', #89549 ) ;
#97240=DIRECTION ( 'NONE',  ( 0.6830127018922181881, 0.6830127018922202975, -0.2588190451025214056 ) ) ;
#97241=CARTESIAN_POINT ( 'NONE',  ( -25.49999999999981881, -1.912538124160733766, 4.000000000000000000 ) ) ;
#97242=ORIENTED_EDGE ( 'NONE', *, *, #121411, .T. ) ;
#97243=VECTOR ( 'NONE', #64034, 1000.000000000000000 ) ;
#97244=DIRECTION ( 'NONE',  ( 0.7071067811865487940, -0.7071067811865463515, 0.000000000000000000 ) ) ;
#97246=CARTESIAN_POINT ( 'NONE',  ( 22.74845587132411140, -11.24070752338416845, 10.39518518046004125 ) ) ;
#97247=DIRECTION ( 'NONE',  ( -0.7071067811865486830, 0.7071067811865464625, 0.000000000000000000 ) ) ;
#97248=ORIENTED_EDGE ( 'NONE', *, *, #48085, .T. ) ;
#97249=ORIENTED_EDGE ( 'NONE', *, *, #13486, .F. ) ;
#97250=VECTOR ( 'NONE', #19030, 999.9999999999998863 ) ;
#97251=ORIENTED_EDGE ( 'NONE', *, *, #5477, .T. ) ;
#97252=CARTESIAN_POINT ( 'NONE',  ( -27.78162688292475124, 21.74787736706806740, 4.999607392498048419 ) ) ;
#97253=DIRECTION ( 'NONE',  ( 0.7071067811865487940, 0.7071067811865463515, 0.000000000000000000 ) ) ;
#97254=EDGE_LOOP ( 'NONE', ( #72140, #38494, #98432 ) ) ;
#97255=ORIENTED_EDGE ( 'NONE', *, *, #20239, .T. ) ;
#97256=VERTEX_POINT ( 'NONE', #35204 ) ;
#97257=DIRECTION ( 'NONE',  ( 0.7071067811865487940, 0.7071067811865463515, -0.000000000000000000 ) ) ;
#97258=CARTESIAN_POINT ( 'NONE',  ( 4.499999999999968914, -11.56887692260769995, 4.000000000000000000 ) ) ;
#97259=EDGE_CURVE ( 'NONE', #47109, #38139, #90255, .T. ) ;
#97261=DIRECTION ( 'NONE',  ( 0.7071067811865487940, 0.7071067811865463515, 0.000000000000000000 ) ) ;
#97263=LINE ( 'NONE', #141534, #39367 ) ;
#97264=VECTOR ( 'NONE', #56230, 1000.000000000000000 ) ;
#97265=PLANE ( 'NONE',  #74565 ) ;
#97268=ORIENTED_EDGE ( 'NONE', *, *, #136185, .F. ) ;
#97271=DIRECTION ( 'NONE',  ( 0.7071067811865486830, -0.7071067811865464625, -0.000000000000000000 ) ) ;
#97272=DIRECTION ( 'NONE',  ( 0.7071067811865486830, -0.7071067811865464625, -0.000000000000000000 ) ) ;
#97273=LINE ( 'NONE', #99431, #868 ) ;
#97274=ORIENTED_EDGE ( 'NONE', *, *, #140656, .T. ) ;
#97276=ORIENTED_EDGE ( 'NONE', *, *, #39444, .F. ) ;
#97277=CARTESIAN_POINT ( 'NONE',  ( 0.000000000000000000, 0.000000000000000000, 5.000000000000000000 ) ) ;
#97278=VECTOR ( 'NONE', #1211, 1000.000000000000000 ) ;
#97279=CARTESIAN_POINT ( 'NONE',  ( 29.99999999999979039, -0.03360074219773898085, 5.000000000000000000 ) ) ;
#97280=CARTESIAN_POINT ( 'NONE',  ( -47.99451991528749062, 28.92564299267971251, 4.000000000000000000 ) ) ;
#97281=EDGE_CURVE ( 'NONE', #90791, #60163, #36588, .T. ) ;
#97282=ORIENTED_EDGE ( 'NONE', *, *, #86189, .T. ) ;
#97285=LINE ( 'NONE', #65447, #113665 ) ;
#97286=DIRECTION ( 'NONE',  ( 0.7071067811865486830, -0.7071067811865464625, -0.000000000000000000 ) ) ;
#97288=VECTOR ( 'NONE', #91958, 999.9999999999998863 ) ;
#97289=ADVANCED_FACE ( 'NONE', ( #46080 ), #125032, .F. ) ;
#97290=VECTOR ( 'NONE', #3008, 1000.000000000000000 ) ;
#97291=AXIS2_PLACEMENT_3D ( 'NONE', #21562, #12092, #65823 ) ;
#97292=PLANE ( 'NONE',  #46273 ) ;
#97293=AXIS2_PLACEMENT_3D ( 'NONE', #113261, #24837, #137191 ) ;
#97295=CIRCLE ( 'NONE', #83372, 0.5000000000000004441 ) ;
#97296=VERTEX_POINT ( 'NONE', #133093 ) ;
#97297=CARTESIAN_POINT ( 'NONE',  ( -20.99999999999984723, -16.06887692260765377, 4.000000000000000000 ) ) ;
#97298=LINE ( 'NONE', #95903, #83219 ) ;
#97299=ORIENTED_EDGE ( 'NONE', *, *, #53758, .F. ) ;
#97300=ORIENTED_EDGE ( 'NONE', *, *, #93397, .F. ) ;
#97301=PLANE ( 'NONE',  #98191 ) ;
#97302=AXIS2_PLACEMENT_3D ( 'NONE', #66033, #54444, #110198 ) ;
#97303=CARTESIAN_POINT ( 'NONE',  ( -3.707106781186512823, -6.740707523384214639, 5.000000000000000000 ) ) ;
#97306=LINE ( 'NONE', #99457, #43637 ) ;
#97308=VERTEX_POINT ( 'NONE', #14838 ) ;
#97309=ADVANCED_FACE ( 'NONE', ( #112730 ), #59114, .F. ) ;
#97310=LINE ( 'NONE', #29935, #88401 ) ;
#97312=VECTOR ( 'NONE', #129638, 1000.000000000000227 ) ;
#97313=DIRECTION ( 'NONE',  ( 0.000000000000000000, 1.000000000000000000, 0.000000000000000000 ) ) ;
#97315=LINE ( 'NONE', #141586, #23241 ) ;
#97316=EDGE_CURVE ( 'NONE', #10400, #100160, #67849, .T. ) ;
#97317=EDGE_CURVE ( 'NONE', #51470, #49172, #3918, .T. ) ;
#97318=AXIS2_PLACEMENT_3D ( 'NONE', #123130, #67316, #33973 ) ;
#97319=EDGE_LOOP ( 'NONE', ( #32822, #117883, #105974, #184, #43106, #118890 ) ) ;
#97320=LINE ( 'NONE', #108194, #97349 ) ;
#97321=AXIS2_PLACEMENT_3D ( 'NONE', #78569, #122765, #23452 ) ;
#97322=EDGE_LOOP ( 'NONE', ( #50837, #111044, #126845, #134992 ) ) ;
#97323=AXIS2_PLACEMENT_3D ( 'NONE', #91354, #113063, #23941 ) ;
#97324=ORIENTED_EDGE ( 'NONE', *, *, #120253, .F. ) ;
#97325=LINE ( 'NONE', #66181, #22347 ) ;
#97326=CARTESIAN_POINT ( 'NONE',  ( 21.29974487139158512, -27.71228299555221142, 4.000000000000000000 ) ) ;
#97327=VECTOR ( 'NONE', #54757, 1000.000000000000000 ) ;
#97328=EDGE_CURVE ( 'NONE', #126851, #13117, #111288, .T. ) ;
#97330=FACE_OUTER_BOUND ( 'NONE', #70599, .T. ) ;
#97331=CARTESIAN_POINT ( 'NONE',  ( -42.29974487139158157, -27.71228299555235708, 4.000000000000000000 ) ) ;
#97332=LINE ( 'NONE', #40172, #67179 ) ;
#97333=EDGE_CURVE ( 'NONE', #4583, #22939, #56264, .T. ) ;
#97337=ORIENTED_EDGE ( 'NONE', *, *, #51859, .F. ) ;
#97338=EDGE_CURVE ( 'NONE', #103228, #19198, #101854, .T. ) ;
#97339=PLANE ( 'NONE',  #20973 ) ;
#97340=LINE ( 'NONE', #96615, #70054 ) ;
#97341=PLANE ( 'NONE',  #38057 ) ;
#97343=CARTESIAN_POINT ( 'NONE',  ( 5.510786437626906675, -27.52281430457051314, 5.000000000000000000 ) ) ;
#97344=CARTESIAN_POINT ( 'NONE',  ( -14.99999999999989875, -1.209798855135683748, 4.371887122346860721 ) ) ;
#97345=CARTESIAN_POINT ( 'NONE',  ( 50.99451991528749062, 28.92564299267973738, 4.000000000000000000 ) ) ;
#97347=EDGE_CURVE ( 'NONE', #28576, #25994, #102955, .T. ) ;
#97348=LINE ( 'NONE', #86525, #106322 ) ;
#97349=VECTOR ( 'NONE', #128564, 999.9999999999998863 ) ;
#97351=EDGE_LOOP ( 'NONE', ( #100667, #138358, #13866, #65599 ) ) ;
#97353=EDGE_CURVE ( 'NONE', #72881, #135979, #78682, .T. ) ;
#97354=CARTESIAN_POINT ( 'NONE',  ( -29.72174548431409136, 8.259292476615641476, 11.78515199841143435 ) ) ;
#97355=LINE ( 'NONE', #31428, #30002 ) ;
#97360=CARTESIAN_POINT ( 'NONE',  ( 23.29289321881330110, -18.74070752338408852, 5.000000000000000000 ) ) ;
#97362=ORIENTED_EDGE ( 'NONE', *, *, #50056, .T. ) ;
#97364=VERTEX_POINT ( 'NONE', #82270 ) ;
#97365=ORIENTED_EDGE ( 'NONE', *, *, #136413, .T. ) ;
#97367=AXIS2_PLACEMENT_3D ( 'NONE', #122615, #23285, #1523 ) ;
#97368=CARTESIAN_POINT ( 'NONE',  ( 21.48921356237309155, -27.52281430457070499, 5.000000000000000000 ) ) ;
#97369=DIRECTION ( 'NONE',  ( 1.000000000000000000, -0.000000000000000000, -0.000000000000000000 ) ) ;
#97370=DIRECTION ( 'NONE',  ( -0.7071067811865486830, -0.7071067811865464625, 0.000000000000000000 ) ) ;
#97371=LINE ( 'NONE', #32897, #16191 ) ;
#97372=ORIENTED_EDGE ( 'NONE', *, *, #96316, .T. ) ;
#97373=PLANE ( 'NONE',  #45256 ) ;
#97374=CARTESIAN_POINT ( 'NONE',  ( -7.171830600776425868, 3.759292476615678336, 4.000000000000000000 ) ) ;
#97376=EDGE_LOOP ( 'NONE', ( #142422, #11840, #35960, #117565 ) ) ;
#97378=CARTESIAN_POINT ( 'NONE',  ( -23.51078643762690490, -27.52281430457038880, 5.000000000000000000 ) ) ;
#97379=CARTESIAN_POINT ( 'NONE',  ( -26.67183060077628198, -15.74070752338411694, 4.000000000000000000 ) ) ;
#97381=ADVANCED_FACE ( 'NONE', ( #29283 ), #40206, .F. ) ;
#97382=VECTOR ( 'NONE', #64746, 1000.000000000000000 ) ;
#97383=DIRECTION ( 'NONE',  ( 0.7071067811865487940, 0.7071067811865463515, 0.000000000000000000 ) ) ;
#97384=ADVANCED_FACE ( 'NONE', ( #18378 ), #72853, .F. ) ;
#97385=ADVANCED_FACE ( 'NONE', ( #73526 ), #28596, .F. ) ;
#97386=ORIENTED_EDGE ( 'NONE', *, *, #126518, .T. ) ;
#97389=LINE ( 'NONE', #8917, #30258 ) ;
#97390=LINE ( 'NONE', #83726, #52433 ) ;
#97391=ORIENTED_EDGE ( 'NONE', *, *, #73034, .F. ) ;
#97392=VERTEX_POINT ( 'NONE', #117688 ) ;
#97393=CARTESIAN_POINT ( 'NONE',  ( 11.48334561358946360, 22.22500000000000142, 4.500000000000000888 ) ) ;
#97394=DIRECTION ( 'NONE',  ( -0.7071067811865486830, -0.7071067811865464625, 0.000000000000000000 ) ) ;
#97395=VECTOR ( 'NONE', #91927, 1000.000000000000000 ) ;
#97396=EDGE_CURVE ( 'NONE', #104452, #5522, #61949, .T. ) ;
#97397=ORIENTED_EDGE ( 'NONE', *, *, #132739, .F. ) ;
#97398=( BOUNDED_CURVE ( )  B_SPLINE_CURVE ( 3, ( #93997, #59284, #127348, #25903 ),
 .UNSPECIFIED., .F., .F. ) 
 B_SPLINE_CURVE_WITH_KNOTS ( ( 4, 4 ),
 ( 5.920967161967926273, 7.341195215986645373 ),
 .UNSPECIFIED. ) 
 CURVE ( )  GEOMETRIC_REPRESENTATION_ITEM ( )  RATIONAL_B_SPLINE_CURVE ( ( 1.000000000000000000, 0.8388583629366594963, 0.8388583629366594963, 1.000000000000000000 ) ) 
 REPRESENTATION_ITEM ( '' )  );
#97400=VECTOR ( 'NONE', #98491, 999.9999999999998863 ) ;
#97402=LINE ( 'NONE', #130070, #97656 ) ;
#97403=EDGE_LOOP ( 'NONE', ( #91624, #26723, #67345, #138565 ) ) ;
#97404=CARTESIAN_POINT ( 'NONE',  ( -31.82816939922330945, -17.24070752338410628, 4.000000000000000000 ) ) ;
#97407=VECTOR ( 'NONE', #9976, 1000.000000000000000 ) ;
#97408=VECTOR ( 'NONE', #21399, 1000.000000000000000 ) ;
#97409=VECTOR ( 'NONE', #66341, 1000.000000000000227 ) ;
#97412=CARTESIAN_POINT ( 'NONE',  ( 84.48921356237309510, -27.52281430457114197, 5.000000000000000000 ) ) ;
#97413=FACE_BOUND ( 'NONE', #96462, .T. ) ;
#97414=LINE ( 'NONE', #96684, #89563 ) ;
#97416=AXIS2_PLACEMENT_3D ( 'NONE', #130220, #51945, #62833 ) ;
#97417=LINE ( 'NONE', #87287, #91963 ) ;
#97418=PLANE ( 'NONE',  #143082 ) ;
#97419=ORIENTED_EDGE ( 'NONE', *, *, #75699, .F. ) ;
#97420=CARTESIAN_POINT ( 'NONE',  ( -13.82816939922343380, -20.24070752338408141, 4.000000000000000000 ) ) ;
#97422=VERTEX_POINT ( 'NONE', #106101 ) ;
#97423=ORIENTED_EDGE ( 'NONE', *, *, #7259, .T. ) ;
#97425=ORIENTED_EDGE ( 'NONE', *, *, #135286, .F. ) ;
#97428=DIRECTION ( 'NONE',  ( -0.000000000000000000, 0.3543493200069153248, 0.9351131265310292928 ) ) ;
#97429=EDGE_CURVE ( 'NONE', #49762, #24456, #93832, .T. ) ;
#97430=VECTOR ( 'NONE', #125895, 1000.000000000000000 ) ;
#97432=DIRECTION ( 'NONE',  ( 0.6830127018922180770, -0.6830127018922204085, -0.2588190451025213501 ) ) ;
#97433=AXIS2_PLACEMENT_3D ( 'NONE', #63931, #42193, #31304 ) ;
#97434=CARTESIAN_POINT ( 'NONE',  ( 2.510786437626908008, -27.52281430457053446, 5.000000000000000000 ) ) ;
#97435=PLANE ( 'NONE',  #66922 ) ;
#97436=VECTOR ( 'NONE', #71760, 1000.000000000000227 ) ;
#97437=DIRECTION ( 'NONE',  ( 0.6830127018922180770, -0.6830127018922204085, -0.2588190451025213501 ) ) ;
#97438=DIRECTION ( 'NONE',  ( -0.7071067811865487940, 0.7071067811865463515, 0.000000000000000000 ) ) ;
#97439=CARTESIAN_POINT ( 'NONE',  ( -51.18398860626899705, 28.73617430169823095, 5.000000000000000000 ) ) ;
#97440=AXIS2_PLACEMENT_3D ( 'NONE', #65221, #22365, #99964 ) ;
#97443=ORIENTED_EDGE ( 'NONE', *, *, #136802, .F. ) ;
#97444=CARTESIAN_POINT ( 'NONE',  ( -15.18398860626900237, 28.73617430169797871, 5.000000000000000000 ) ) ;
#97445=EDGE_LOOP ( 'NONE', ( #23794, #51519, #41123, #21039 ) ) ;
#97446=VECTOR ( 'NONE', #113209, 1000.000000000000000 ) ;
#97448=PLANE ( 'NONE',  #46678 ) ;
#97449=EDGE_CURVE ( 'NONE', #11291, #57481, #48195, .T. ) ;
#97450=ORIENTED_EDGE ( 'NONE', *, *, #115020, .T. ) ;
#97453=AXIS2_PLACEMENT_3D ( 'NONE', #44432, #108906, #110338 ) ;
#97456=EDGE_LOOP ( 'NONE', ( #123114, #86609, #18299, #70287 ) ) ;
#97458=EDGE_CURVE ( 'NONE', #58779, #115678, #84413, .T. ) ;
#97464=EDGE_LOOP ( 'NONE', ( #107230, #64085, #120383, #13053 ) ) ;
#97465=CARTESIAN_POINT ( 'NONE',  ( -26.20710678118635784, -5.240707523384228850, 5.000000000000000000 ) ) ;
#97466=AXIS2_PLACEMENT_3D ( 'NONE', #30910, #97561, #30166 ) ;
#97467=DIRECTION ( 'NONE',  ( -0.3543493200069162685, -0.000000000000000000, -0.9351131265310288487 ) ) ;
#97468=DIRECTION ( 'NONE',  ( -0.000000000000000000, 0.3543493200069153248, 0.9351131265310292928 ) ) ;
#97469=ORIENTED_EDGE ( 'NONE', *, *, #97030, .F. ) ;
#97471=ORIENTED_EDGE ( 'NONE', *, *, #53407, .T. ) ;
#97472=CARTESIAN_POINT ( 'NONE',  ( -22.82816939922337340, 9.759292476615620160, 4.000000000000000000 ) ) ;
#97473=DIRECTION ( 'NONE',  ( 0.7071067811865486830, -0.7071067811865464625, -0.000000000000000000 ) ) ;
#97474=CARTESIAN_POINT ( 'NONE',  ( -9.183988606268997046, 28.73617430169793607, 5.000000000000000000 ) ) ;
#97476=VERTEX_POINT ( 'NONE', #94529 ) ;
#97478=ORIENTED_EDGE ( 'NONE', *, *, #38948, .T. ) ;
#97479=ORIENTED_EDGE ( 'NONE', *, *, #75626, .F. ) ;
#97480=ORIENTED_EDGE ( 'NONE', *, *, #136417, .T. ) ;
#97481=LINE ( 'NONE', #87347, #21747 ) ;
#97482=VECTOR ( 'NONE', #65809, 1000.000000000000000 ) ;
#97484=CARTESIAN_POINT ( 'NONE',  ( 30.45983838949721090, 18.75929247661552424, 8.305906642995555700 ) ) ;
#97486=DIRECTION ( 'NONE',  ( 1.000000000000000000, 0.000000000000000000, 0.000000000000000000 ) ) ;
#97488=ORIENTED_EDGE ( 'NONE', *, *, #85662, .T. ) ;
#97490=ORIENTED_EDGE ( 'NONE', *, *, #8612, .T. ) ;
#97491=ADVANCED_FACE ( 'NONE', ( #93127 ), #83711, .F. ) ;
#97492=VECTOR ( 'NONE', #87758, 1000.000000000000000 ) ;
#97493=DIRECTION ( 'NONE',  ( 0.7071067811865486830, -0.7071067811865464625, -0.000000000000000000 ) ) ;
#97494=DIRECTION ( 'NONE',  ( 0.3543493200069162685, -0.000000000000000000, -0.9351131265310288487 ) ) ;
#97495=EDGE_LOOP ( 'NONE', ( #20058, #128108, #44835, #115777, #133280 ) ) ;
#97496=PLANE ( 'NONE',  #110852 ) ;
#97497=CARTESIAN_POINT ( 'NONE',  ( 0.000000000000000000, 0.000000000000000000, 5.000000000000000000 ) ) ;
#97498=ORIENTED_EDGE ( 'NONE', *, *, #138137, .F. ) ;
#97499=ORIENTED_EDGE ( 'NONE', *, *, #122396, .T. ) ;
#97501=DIRECTION ( 'NONE',  ( 0.7071067811865487940, 0.7071067811865463515, 0.000000000000000000 ) ) ;
#97503=CARTESIAN_POINT ( 'NONE',  ( 0.2997448713915885632, -27.71228299555206220, 4.000000000000000000 ) ) ;
#97504=LINE ( 'NONE', #42466, #26565 ) ;
#97505=VECTOR ( 'NONE', #122624, 1000.000000000000227 ) ;
#97506=CARTESIAN_POINT ( 'NONE',  ( -21.18398860626899349, 28.73617430169802134, 5.000000000000000000 ) ) ;
#97508=DIRECTION ( 'NONE',  ( -0.7071067811865487940, 0.7071067811865463515, 0.000000000000000000 ) ) ;
#97510=EDGE_CURVE ( 'NONE', #141681, #63322, #71381, .T. ) ;
#97513=FACE_OUTER_BOUND ( 'NONE', #54194, .T. ) ;
#97514=FACE_OUTER_BOUND ( 'NONE', #111830, .T. ) ;
#97515=EDGE_CURVE ( 'NONE', #126442, #102417, #74971, .T. ) ;
#97516=ORIENTED_EDGE ( 'NONE', *, *, #64484, .F. ) ;
#97517=CARTESIAN_POINT ( 'NONE',  ( -29.99999999999977973, 2.587461875839211167, 4.000000000000000000 ) ) ;
#97519=AXIS2_PLACEMENT_3D ( 'NONE', #82545, #15799, #113740 ) ;
#97521=AXIS2_PLACEMENT_3D ( 'NONE', #26043, #117295, #126077 ) ;
#97522=CARTESIAN_POINT ( 'NONE',  ( 12.00548008471251293, 28.92564299267929684, 4.000000000000000000 ) ) ;
#97524=CARTESIAN_POINT ( 'NONE',  ( -29.29289321881324781, -6.740707523384214639, 5.000000000000000000 ) ) ;
#97525=ORIENTED_EDGE ( 'NONE', *, *, #14537, .F. ) ;
#97526=EDGE_CURVE ( 'NONE', #34599, #89628, #86546, .T. ) ;
#97528=CARTESIAN_POINT ( 'NONE',  ( 0.000000000000000000, 0.000000000000000000, 5.000000000000000000 ) ) ;
#97529=CARTESIAN_POINT ( 'NONE',  ( -5.207106781186502609, -2.240707523384259492, 5.000000000000000000 ) ) ;
#97530=ORIENTED_EDGE ( 'NONE', *, *, #108591, .F. ) ;
#97531=PLANE ( 'NONE',  #94882 ) ;
#97532=CARTESIAN_POINT ( 'NONE',  ( 34.75611968250419892, -21.18706574529238651, 4.955485411084882941 ) ) ;
#97533=DIRECTION ( 'NONE',  ( 0.3543493200069162685, -0.000000000000000000, -0.9351131265310288487 ) ) ;
#97534=VERTEX_POINT ( 'NONE', #129302 ) ;
#97535=VERTEX_POINT ( 'NONE', #43737 ) ;
#97536=LINE ( 'NONE', #78659, #78748 ) ;
#97537=CARTESIAN_POINT ( 'NONE',  ( -9.874853806907596621, -14.24070752338414003, 9.401115078912679834 ) ) ;
#97538=AXIS2_PLACEMENT_3D ( 'NONE', #95254, #120544, #21273 ) ;
#97540=DIRECTION ( 'NONE',  ( -0.7071067811865486830, -0.7071067811865464625, -0.000000000000000000 ) ) ;
#97542=LINE ( 'NONE', #106989, #6953 ) ;
#97543=LINE ( 'NONE', #143201, #78440 ) ;
#97544=VERTEX_POINT ( 'NONE', #75663 ) ;
#97545=VECTOR ( 'NONE', #71783, 1000.000000000000000 ) ;
#97546=ADVANCED_FACE ( 'NONE', ( #10374 ), #132197, .T. ) ;
#97547=DIRECTION ( 'NONE',  ( 0.7071067811865487940, 0.7071067811865463515, -0.000000000000000000 ) ) ;
#97548=CARTESIAN_POINT ( 'NONE',  ( -34.92500000000001137, 22.22500000000000142, 4.000000000000000000 ) ) ;
#97550=ORIENTED_EDGE ( 'NONE', *, *, #7212, .F. ) ;
#97551=EDGE_CURVE ( 'NONE', #140592, #97230, #130776, .T. ) ;
#97552=PLANE ( 'NONE',  #132452 ) ;
#97553=ORIENTED_EDGE ( 'NONE', *, *, #47782, .F. ) ;
#97554=AXIS2_PLACEMENT_3D ( 'NONE', #36789, #114357, #93320 ) ;
#97556=VECTOR ( 'NONE', #39374, 1000.000000000000000 ) ;
#97558=LINE ( 'NONE', #19297, #26129 ) ;
#97559=VERTEX_POINT ( 'NONE', #140888 ) ;
#97560=AXIS2_PLACEMENT_3D ( 'NONE', #13011, #13714, #136228 ) ;
#97561=DIRECTION ( 'NONE',  ( 0.6830127018922181881, 0.6830127018922202975, -0.2588190451025214056 ) ) ;
#97562=DIRECTION ( 'NONE',  ( -0.7071067811865486830, -0.7071067811865464625, 0.000000000000000000 ) ) ;
#97563=LINE ( 'NONE', #10540, #94852 ) ;
#97564=VECTOR ( 'NONE', #106246, 1000.000000000000000 ) ;
#97566=CARTESIAN_POINT ( 'NONE',  ( 34.45011844616453800, -2.997695858406035363, 5.000000000000001776 ) ) ;
#97567=ORIENTED_EDGE ( 'NONE', *, *, #76926, .T. ) ;
#97568=CARTESIAN_POINT ( 'NONE',  ( -45.48921356237309510, -27.52281430457087197, 5.000000000000000000 ) ) ;
#97569=DIRECTION ( 'NONE',  ( -0.7071067811865486830, -0.7071067811865464625, -0.000000000000000000 ) ) ;
#97570=PLANE ( 'NONE',  #86447 ) ;
#97572=ORIENTED_EDGE ( 'NONE', *, *, #12573, .T. ) ;
#97573=EDGE_CURVE ( 'NONE', #121799, #42327, #76378, .T. ) ;
#97574=VERTEX_POINT ( 'NONE', #9663 ) ;
#97577=LINE ( 'NONE', #85268, #31427 ) ;
#97578=CARTESIAN_POINT ( 'NONE',  ( -20.70025512860841133, -27.71228299555191654, 4.000000000000000000 ) ) ;
#97579=AXIS2_PLACEMENT_3D ( 'NONE', #82802, #16813, #61089 ) ;
#97580=CARTESIAN_POINT ( 'NONE',  ( 8.671830600776411657, 5.259292476615662792, 4.000000000000000000 ) ) ;
#97581=CARTESIAN_POINT ( 'NONE',  ( 34.92499999999998295, -21.72500000000000142, 5.000000000000000000 ) ) ;
#97582=VERTEX_POINT ( 'NONE', #119144 ) ;
#97583=VECTOR ( 'NONE', #12468, 1000.000000000000114 ) ;
#97584=CARTESIAN_POINT ( 'NONE',  ( -15.29974487139158867, -27.71228299555216879, 4.000000000000000000 ) ) ;
#97585=EDGE_LOOP ( 'NONE', ( #24855, #75190, #50329, #41459 ) ) ;
#97586=CARTESIAN_POINT ( 'NONE',  ( 33.48921356237309510, -27.52281430457078670, 5.000000000000000000 ) ) ;
#97587=CARTESIAN_POINT ( 'NONE',  ( -34.92500000000001137, 22.22500000000000142, 4.000000000000000000 ) ) ;
#97588=LINE ( 'NONE', #120028, #35445 ) ;
#97589=VECTOR ( 'NONE', #132314, 1000.000000000000000 ) ;
#97590=ORIENTED_EDGE ( 'NONE', *, *, #47557, .T. ) ;
#97591=VERTEX_POINT ( 'NONE', #87955 ) ;
#97592=FACE_BOUND ( 'NONE', #35689, .T. ) ;
#97593=LINE ( 'NONE', #30949, #1468 ) ;
#97594=CARTESIAN_POINT ( 'NONE',  ( 36.18398860626899705, 28.73617430169812437, 5.000000000000000000 ) ) ;
#97595=PLANE ( 'NONE',  #131607 ) ;
#97598=( BOUNDED_CURVE ( )  B_SPLINE_CURVE ( 3, ( #128562, #53114, #130726, #72807 ),
 .UNSPECIFIED., .F., .T. ) 
 B_SPLINE_CURVE_WITH_KNOTS ( ( 4, 4 ),
 ( 5.005968288816742273, 5.074607125596344304 ),
 .UNSPECIFIED. ) 
 CURVE ( )  GEOMETRIC_REPRESENTATION_ITEM ( )  RATIONAL_B_SPLINE_CURVE ( ( 1.000000000000000000, 0.9996074310407765395, 0.9996074310407765395, 1.000000000000000000 ) ) 
 REPRESENTATION_ITEM ( '' )  );
#97599=DIRECTION ( 'NONE',  ( 0.7071067811865486830, -0.7071067811865464625, -0.000000000000000000 ) ) ;
#97601=ORIENTED_EDGE ( 'NONE', *, *, #66567, .T. ) ;
#97603=ORIENTED_EDGE ( 'NONE', *, *, #141252, .T. ) ;
#97604=EDGE_LOOP ( 'NONE', ( #34264, #19983, #40100, #26363 ) ) ;
#97605=AXIS2_PLACEMENT_3D ( 'NONE', #83823, #125140, #114940 ) ;
#97607=CARTESIAN_POINT ( 'NONE',  ( 15.41161490594821437, 22.22500000000000142, 4.777194822843815913 ) ) ;
#97610=DIRECTION ( 'NONE',  ( -0.7071067811865486830, -0.7071067811865464625, 0.000000000000000000 ) ) ;
#97611=ORIENTED_EDGE ( 'NONE', *, *, #14906, .F. ) ;
#97612=FACE_OUTER_BOUND ( 'NONE', #106861, .T. ) ;
#97613=CARTESIAN_POINT ( 'NONE',  ( -2.994519915287485734, 28.92564299267940342, 4.000000000000000000 ) ) ;
#97614=DIRECTION ( 'NONE',  ( 0.6830127018922180770, -0.6830127018922204085, -0.2588190451025213501 ) ) ;
#97615=DIRECTION ( 'NONE',  ( 0.3543493200069162685, -0.000000000000000000, -0.9351131265310288487 ) ) ;
#97616=ADVANCED_FACE ( 'NONE', ( #109706 ), #74231, .F. ) ;
#97618=VECTOR ( 'NONE', #135352, 1000.000000000000000 ) ;
#97619=VECTOR ( 'NONE', #111825, 1000.000000000000000 ) ;
#97621=VECTOR ( 'NONE', #50529, 999.9999999999998863 ) ;
#97622=LINE ( 'NONE', #11299, #86077 ) ;
#97623=VERTEX_POINT ( 'NONE', #32150 ) ;
#97624=AXIS2_PLACEMENT_3D ( 'NONE', #69715, #71851, #15966 ) ;
#97625=PLANE ( 'NONE',  #132963 ) ;
#97626=FACE_OUTER_BOUND ( 'NONE', #55851, .T. ) ;
#97627=EDGE_CURVE ( 'NONE', #37692, #92938, #97371, .T. ) ;
#97628=ORIENTED_EDGE ( 'NONE', *, *, #32397, .T. ) ;
#97629=CARTESIAN_POINT ( 'NONE',  ( -0.2997448713915885632, -27.71228299555206220, 4.000000000000000000 ) ) ;
#97630=ORIENTED_EDGE ( 'NONE', *, *, #16544, .T. ) ;
#97631=VERTEX_POINT ( 'NONE', #21274 ) ;
#97632=EDGE_CURVE ( 'NONE', #134215, #43029, #21973, .T. ) ;
#97633=EDGE_CURVE ( 'NONE', #43477, #139296, #53933, .T. ) ;
#97634=ORIENTED_EDGE ( 'NONE', *, *, #9256, .F. ) ;
#97637=ORIENTED_EDGE ( 'NONE', *, *, #106699, .T. ) ;
#97638=ORIENTED_EDGE ( 'NONE', *, *, #74422, .T. ) ;
#97642=DIRECTION ( 'NONE',  ( -0.6830127018922180770, -0.6830127018922204085, -0.2588190451025213501 ) ) ;
#97644=CARTESIAN_POINT ( 'NONE',  ( -18.78162688292481874, 21.74787736706806385, 4.999607392498049308 ) ) ;
#97645=ADVANCED_FACE ( 'NONE', ( #22658 ), #123478, .F. ) ;
#97646=CARTESIAN_POINT ( 'NONE',  ( -1.499999999999987566, 16.46639925780209168, 5.000000000000000000 ) ) ;
#97647=ORIENTED_EDGE ( 'NONE', *, *, #88853, .F. ) ;
#97648=DIRECTION ( 'NONE',  ( 0.7071067811865487940, -0.7071067811865463515, 0.000000000000000000 ) ) ;
#97649=EDGE_CURVE ( 'NONE', #62399, #51414, #23399, .T. ) ;
#97650=CARTESIAN_POINT ( 'NONE',  ( 24.99941145866615244, 2.672864951410429679, 4.679979323531649804 ) ) ;
#97653=CARTESIAN_POINT ( 'NONE',  ( 0.000000000000000000, 0.000000000000000000, 5.000000000000000000 ) ) ;
#97654=EDGE_CURVE ( 'NONE', #102314, #86645, #112262, .T. ) ;
#97655=VERTEX_POINT ( 'NONE', #13940 ) ;
#97656=VECTOR ( 'NONE', #43073, 1000.000000000000000 ) ;
#97657=CARTESIAN_POINT ( 'NONE',  ( -34.92500000000001137, -19.48753812416029874, 4.000000000000000000 ) ) ;
#97658=EDGE_LOOP ( 'NONE', ( #116797, #134327, #106864, #54338 ) ) ;
#97659=VECTOR ( 'NONE', #64335, 999.9999999999998863 ) ;
#97660=ORIENTED_EDGE ( 'NONE', *, *, #101785, .T. ) ;
#97661=ORIENTED_EDGE ( 'NONE', *, *, #141591, .F. ) ;
#97665=CARTESIAN_POINT ( 'NONE',  ( 11.99999999999991296, 14.87792677143810316, -11.06722581663437488 ) ) ;
#97666=DIRECTION ( 'NONE',  ( 0.7071067811865487940, -0.7071067811865463515, 0.000000000000000000 ) ) ;
#97667=EDGE_CURVE ( 'NONE', #40996, #99872, #34292, .T. ) ;
#97668=CARTESIAN_POINT ( 'NONE',  ( -27.79289321881325492, 15.75929247661555799, 5.000000000000000000 ) ) ;
#97669=VERTEX_POINT ( 'NONE', #111105 ) ;
#97672=ADVANCED_FACE ( 'NONE', ( #57495 ), #189, .F. ) ;
#97675=DIRECTION ( 'NONE',  ( 0.7071067811865487940, 0.7071067811865463515, 0.000000000000000000 ) ) ;
#97676=CARTESIAN_POINT ( 'NONE',  ( -14.99999999999988809, -1.447814304570818500, 5.000000000000000000 ) ) ;
#97677=CARTESIAN_POINT ( 'NONE',  ( 34.47516574401891631, 3.028067341115785460, 4.998110765256834398 ) ) ;
#97678=EDGE_LOOP ( 'NONE', ( #15307, #54718, #47797, #106811 ) ) ;
#97679=ORIENTED_EDGE ( 'NONE', *, *, #82760, .F. ) ;
#97680=AXIS2_PLACEMENT_3D ( 'NONE', #101333, #58608, #123827 ) ;
#97681=ADVANCED_FACE ( 'NONE', ( #45903 ), #58241, .F. ) ;
#97683=DIRECTION ( 'NONE',  ( -0.7071067811865487940, 0.7071067811865463515, -0.000000000000000000 ) ) ;
#97685=VECTOR ( 'NONE', #10849, 1000.000000000000114 ) ;
#97686=CARTESIAN_POINT ( 'NONE',  ( -18.18398860626898994, 28.73617430169800002, 5.000000000000000000 ) ) ;
#97687=PLANE ( 'NONE',  #29750 ) ;
#97688=CARTESIAN_POINT ( 'NONE',  ( -17.67183060077635304, -12.74070752338415602, 4.000000000000000000 ) ) ;
#97690=DIRECTION ( 'NONE',  ( 1.000000000000000000, -0.000000000000000000, -0.000000000000000000 ) ) ;
#97694=ADVANCED_FACE ( 'NONE', ( #47373 ), #134332, .F. ) ;
#97695=ORIENTED_EDGE ( 'NONE', *, *, #135745, .T. ) ;
#97696=CARTESIAN_POINT ( 'NONE',  ( -33.48921356237309510, -27.52281430457078670, 5.000000000000000000 ) ) ;
#97701=EDGE_CURVE ( 'NONE', #51992, #5639, #36438, .T. ) ;
#97702=ADVANCED_FACE ( 'NONE', ( #46653 ), #2338, .F. ) ;
#97704=DIRECTION ( 'NONE',  ( -0.7071067811865486830, -0.7071067811865464625, 0.000000000000000000 ) ) ;
#97706=DIRECTION ( 'NONE',  ( -0.3543493200069162685, -0.000000000000000000, -0.9351131265310288487 ) ) ;
#97707=EDGE_LOOP ( 'NONE', ( #131686, #46604, #87141, #34456 ) ) ;
#97708=LINE ( 'NONE', #86848, #18359 ) ;
#97711=DIRECTION ( 'NONE',  ( 0.7071067811865487940, 0.7071067811865463515, 0.000000000000000000 ) ) ;
#97712=ORIENTED_EDGE ( 'NONE', *, *, #70760, .F. ) ;
#97714=CARTESIAN_POINT ( 'NONE',  ( 34.92499999999998295, 2.816654386410421207, 4.500000000000000888 ) ) ;
#97716=EDGE_CURVE ( 'NONE', #11574, #42096, #25546, .T. ) ;
#97717=CARTESIAN_POINT ( 'NONE',  ( -12.18398860626900060, 28.73617430169795739, 5.000000000000000000 ) ) ;
#97719=CARTESIAN_POINT ( 'NONE',  ( 54.18398860626899705, 28.73617430169825226, 5.000000000000000000 ) ) ;
#97722=VECTOR ( 'NONE', #82226, 999.9999999999998863 ) ;
#97723=AXIS2_PLACEMENT_3D ( 'NONE', #89478, #78615, #35132 ) ;
#97724=VECTOR ( 'NONE', #4275, 1000.000000000000000 ) ;
#97726=CARTESIAN_POINT ( 'NONE',  ( 21.79289321881331531, 18.75929247661553489, 5.000000000000000000 ) ) ;
#97727=ORIENTED_EDGE ( 'NONE', *, *, #89679, .F. ) ;
#97728=ORIENTED_EDGE ( 'NONE', *, *, #120691, .F. ) ;
#97730=AXIS2_PLACEMENT_3D ( 'NONE', #78556, #2369, #122754 ) ;
#97731=DIRECTION ( 'NONE',  ( -0.7071067811865487940, 0.7071067811865463515, 0.000000000000000000 ) ) ;
#97732=EDGE_LOOP ( 'NONE', ( #142748, #98929, #43365, #117174 ) ) ;
#97733=EDGE_CURVE ( 'NONE', #48148, #86443, #91539, .T. ) ;
#97735=DIRECTION ( 'NONE',  ( 0.7071067811865487940, 0.7071067811865463515, 0.000000000000000000 ) ) ;
#97736=CARTESIAN_POINT ( 'NONE',  ( 16.49999999999987921, -20.94781430457061333, 5.000000000000000000 ) ) ;
#97737=VECTOR ( 'NONE', #73676, 1000.000000000000000 ) ;
#97741=ORIENTED_EDGE ( 'NONE', *, *, #60544, .T. ) ;
#97742=LINE ( 'NONE', #73337, #105296 ) ;
#97743=DIRECTION ( 'NONE',  ( 0.3543493200069162685, -0.000000000000000000, -0.9351131265310288487 ) ) ;
#97745=EDGE_CURVE ( 'NONE', #132946, #68806, #924, .T. ) ;
#97747=LINE ( 'NONE', #31780, #100747 ) ;
#97748=ORIENTED_EDGE ( 'NONE', *, *, #129132, .F. ) ;
#97749=CARTESIAN_POINT ( 'NONE',  ( -2.510786437626908008, -27.52281430457053446, 5.000000000000000000 ) ) ;
#97750=LINE ( 'NONE', #141995, #84637 ) ;
#97754=ORIENTED_EDGE ( 'NONE', *, *, #138389, .F. ) ;
#97756=ORIENTED_EDGE ( 'NONE', *, *, #66289, .T. ) ;
#97758=VERTEX_POINT ( 'NONE', #77806 ) ;
#97760=CARTESIAN_POINT ( 'NONE',  ( 42.48921356237308800, -27.52281430457085065, 5.000000000000000000 ) ) ;
#97761=ORIENTED_EDGE ( 'NONE', *, *, #50413, .T. ) ;
#97762=PLANE ( 'NONE',  #70005 ) ;
#97764=EDGE_CURVE ( 'NONE', #99982, #142463, #45207, .T. ) ;
#97765=VECTOR ( 'NONE', #18082, 1000.000000000000000 ) ;
#97767=EDGE_CURVE ( 'NONE', #48205, #90138, #69818, .T. ) ;
#97768=ORIENTED_EDGE ( 'NONE', *, *, #30580, .T. ) ;
#97769=AXIS2_PLACEMENT_3D ( 'NONE', #88236, #33174, #34565 ) ;
#97772=VECTOR ( 'NONE', #11595, 1000.000000000000227 ) ;
#97773=EDGE_LOOP ( 'NONE', ( #135440, #3907, #97661, #23650 ) ) ;
#97774=EDGE_LOOP ( 'NONE', ( #36352, #93851, #35517, #109981 ) ) ;
#97775=EDGE_LOOP ( 'NONE', ( #135240, #72470, #82204, #118511 ) ) ;
#97776=CARTESIAN_POINT ( 'NONE',  ( 44.99451991528749772, 28.92564299267969474, 4.000000000000000000 ) ) ;
#97778=DIRECTION ( 'NONE',  ( 0.7071067811865487940, 0.7071067811865463515, -0.000000000000000000 ) ) ;
#97780=LINE ( 'NONE', #132593, #76652 ) ;
#97783=LINE ( 'NONE', #30387, #2432 ) ;
#97785=ORIENTED_EDGE ( 'NONE', *, *, #143104, .F. ) ;
#97786=VERTEX_POINT ( 'NONE', #92220 ) ;
#97787=CARTESIAN_POINT ( 'NONE',  ( -21.71715331601274102, -2.164967620583693630, 5.000000000000000000 ) ) ;
#97789=EDGE_LOOP ( 'NONE', ( #68991, #4930, #12682 ) ) ;
#97790=AXIS2_PLACEMENT_3D ( 'NONE', #9685, #88716, #98149 ) ;
#97792=LINE ( 'NONE', #606, #5754 ) ;
#97793=EDGE_LOOP ( 'NONE', ( #30519, #136414, #125664, #13697 ) ) ;
#97794=CARTESIAN_POINT ( 'NONE',  ( 39.18398860626899705, 28.73617430169814568, 5.000000000000000000 ) ) ;
#97795=DIRECTION ( 'NONE',  ( -0.7071067811865486830, -0.7071067811865464625, -0.000000000000000000 ) ) ;
#97799=VECTOR ( 'NONE', #18765, 1000.000000000000227 ) ;
#97801=ORIENTED_EDGE ( 'NONE', *, *, #35498, .F. ) ;
#97802=VERTEX_POINT ( 'NONE', #136450 ) ;
#97803=LINE ( 'NONE', #40591, #36572 ) ;
#97804=PLANE ( 'NONE',  #94348 ) ;
#97805=EDGE_LOOP ( 'NONE', ( #34251, #13748, #39897, #119408 ) ) ;
#97806=DIRECTION ( 'NONE',  ( -0.6830127018922181881, 0.6830127018922202975, -0.2588190451025214056 ) ) ;
#97807=ADVANCED_FACE ( 'NONE', ( #16064 ), #60356, .F. ) ;
#97808=ORIENTED_EDGE ( 'NONE', *, *, #73069, .T. ) ;
#97809=PLANE ( 'NONE',  #92156 ) ;
#97810=EDGE_LOOP ( 'NONE', ( #131404, #60399, #42833, #5045 ) ) ;
#97811=VERTEX_POINT ( 'NONE', #71228 ) ;
#97812=AXIS2_PLACEMENT_3D ( 'NONE', #60328, #102404, #36412 ) ;
#97813=ORIENTED_EDGE ( 'NONE', *, *, #57493, .F. ) ;
#97815=EDGE_CURVE ( 'NONE', #17758, #91076, #6603, .T. ) ;
#97816=CARTESIAN_POINT ( 'NONE',  ( -19.49999999999986144, -20.56887692260760758, 4.000000000000000000 ) ) ;
#97818=DIRECTION ( 'NONE',  ( -0.7071067811865487940, 0.7071067811865463515, 0.000000000000000000 ) ) ;
#97819=EDGE_CURVE ( 'NONE', #29477, #69770, #114688, .T. ) ;
#97821=LINE ( 'NONE', #130472, #1040 ) ;
#97822=EDGE_CURVE ( 'NONE', #56334, #38475, #94369, .T. ) ;
#97823=FACE_OUTER_BOUND ( 'NONE', #138361, .T. ) ;
#97824=CARTESIAN_POINT ( 'NONE',  ( -10.95484226663327654, -21.74070752338406720, 21.72585301388582124 ) ) ;
#97825=AXIS2_PLACEMENT_3D ( 'NONE', #107146, #39046, #48495 ) ;
#97826=VECTOR ( 'NONE', #75594, 1000.000000000000000 ) ;
#97827=VECTOR ( 'NONE', #31473, 1000.000000000000227 ) ;
#97828=ADVANCED_FACE ( 'NONE', ( #84255 ), #105256, .T. ) ;
#97829=DIRECTION ( 'NONE',  ( -0.000000000000000000, -0.3543493200069152693, 0.9351131265310292928 ) ) ;
#97830=VECTOR ( 'NONE', #10074, 1000.000000000000000 ) ;
#97831=CARTESIAN_POINT ( 'NONE',  ( 20.67183060077633883, 14.25929247661558286, 4.000000000000000000 ) ) ;
#97832=ADVANCED_FACE ( 'NONE', ( #5203 ), #70543, .F. ) ;
#97833=CARTESIAN_POINT ( 'NONE',  ( -18.48921356237309510, -27.52281430457068367, 5.000000000000000000 ) ) ;
#97834=CARTESIAN_POINT ( 'NONE',  ( -36.18398860626899705, 28.73617430169812437, 5.000000000000000000 ) ) ;
#97835=ADVANCED_FACE ( 'NONE', ( #128453 ), #48752, .F. ) ;
#97837=EDGE_LOOP ( 'NONE', ( #25641, #10310, #57204, #121178 ) ) ;
#97839=VERTEX_POINT ( 'NONE', #126995 ) ;
#97840=VECTOR ( 'NONE', #4070, 999.9999999999998863 ) ;
#97844=ORIENTED_EDGE ( 'NONE', *, *, #82042, .F. ) ;
#97845=ORIENTED_EDGE ( 'NONE', *, *, #35017, .T. ) ;
#97846=CARTESIAN_POINT ( 'NONE',  ( -10.17183060077639922, 6.759292476615645029, 4.000000000000000000 ) ) ;
#97848=ADVANCED_FACE ( 'NONE', ( #17521 ), #61778, .T. ) ;
#97849=EDGE_CURVE ( 'NONE', #137076, #11057, #31284, .T. ) ;
#97850=CARTESIAN_POINT ( 'NONE',  ( -35.99451991528749772, 28.92564299267963079, 4.000000000000000000 ) ) ;
#97851=EDGE_LOOP ( 'NONE', ( #94206, #126410, #38129, #48492 ) ) ;
#97852=CARTESIAN_POINT ( 'NONE',  ( -29.93988928955962336, -9.740707523384187994, 10.89222023123387828 ) ) ;
#97854=EDGE_CURVE ( 'NONE', #108587, #77009, #108788, .T. ) ;
#97855=CARTESIAN_POINT ( 'NONE',  ( 3.850051285410223567, -8.240707523384193323, 17.25253755692239821 ) ) ;
#97856=CARTESIAN_POINT ( 'NONE',  ( -21.18398860626899349, 28.73617430169802134, 5.000000000000000000 ) ) ;
#97857=VECTOR ( 'NONE', #7636, 999.9999999999998863 ) ;
#97859=VERTEX_POINT ( 'NONE', #64609 ) ;
#97861=CARTESIAN_POINT ( 'NONE',  ( -14.51078643762690490, -27.52281430457045275, 5.000000000000000000 ) ) ;
#97862=CARTESIAN_POINT ( 'NONE',  ( -30.18398860626900060, 28.73617430169808173, 5.000000000000000000 ) ) ;
#97863=CARTESIAN_POINT ( 'NONE',  ( -75.18398860626899705, 28.73617430169839793, 5.000000000000000000 ) ) ;
#97864=ORIENTED_EDGE ( 'NONE', *, *, #140890, .T. ) ;
#97865=ORIENTED_EDGE ( 'NONE', *, *, #8982, .F. ) ;
#97866=CARTESIAN_POINT ( 'NONE',  ( -57.48921356237308800, -27.52281430457095368, 5.000000000000000000 ) ) ;
#97869=LINE ( 'NONE', #42795, #55726 ) ;
#97870=CARTESIAN_POINT ( 'NONE',  ( 3.183988606268992161, 28.73617430169789699, 5.000000000000000000 ) ) ;
#97871=LINE ( 'NONE', #52217, #68113 ) ;
#97873=VECTOR ( 'NONE', #12938, 1000.000000000000000 ) ;
#97874=LINE ( 'NONE', #98574, #55331 ) ;
#97876=CARTESIAN_POINT ( 'NONE',  ( -15.09843580608227143, 11.25929247661560240, 10.79108189686403563 ) ) ;
#97877=FACE_OUTER_BOUND ( 'NONE', #10370, .T. ) ;
#97878=EDGE_CURVE ( 'NONE', #56845, #112904, #40728, .T. ) ;
#97880=DIRECTION ( 'NONE',  ( -0.6830127018922180770, -0.6830127018922204085, -0.2588190451025213501 ) ) ;
#97881=VECTOR ( 'NONE', #84410, 1000.000000000000000 ) ;
#97882=AXIS2_PLACEMENT_3D ( 'NONE', #101321, #70175, #134696 ) ;
#97885=CARTESIAN_POINT ( 'NONE',  ( 11.12514619309227193, -14.24070752338413648, 9.401115078912631873 ) ) ;
#97886=ORIENTED_EDGE ( 'NONE', *, *, #54998, .T. ) ;
#97887=ORIENTED_EDGE ( 'NONE', *, *, #77495, .T. ) ;
#97888=DIRECTION ( 'NONE',  ( 0.3543493200069162685, -0.000000000000000000, -0.9351131265310288487 ) ) ;
#97889=FACE_OUTER_BOUND ( 'NONE', #104685, .T. ) ;
#97890=ORIENTED_EDGE ( 'NONE', *, *, #48108, .T. ) ;
#97891=CARTESIAN_POINT ( 'NONE',  ( -10.17183060077640810, -20.24070752338407786, 4.000000000000000000 ) ) ;
#97892=ADVANCED_FACE ( 'NONE', ( #75493 ), #96481, .F. ) ;
#97893=VECTOR ( 'NONE', #96416, 1000.000000000000000 ) ;
#97894=DIRECTION ( 'NONE',  ( 0.7071067811865487940, 0.7071067811865463515, 0.000000000000000000 ) ) ;
#97896=DIRECTION ( 'NONE',  ( 0.7071067811865487940, 0.7071067811865463515, 0.000000000000000000 ) ) ;
#97898=EDGE_CURVE ( 'NONE', #69227, #49314, #127059, .T. ) ;
#97899=DIRECTION ( 'NONE',  ( -0.7071067811865486830, -0.7071067811865464625, 0.000000000000000000 ) ) ;
#97900=AXIS2_PLACEMENT_3D ( 'NONE', #65556, #109726, #30764 ) ;
#97901=CARTESIAN_POINT ( 'NONE',  ( 4.499999999999976019, 13.56627193232215767, -10.57019076586067641 ) ) ;
#97904=CARTESIAN_POINT ( 'NONE',  ( 74.99451991528749772, 28.92564299267990435, 4.000000000000000000 ) ) ;
#97905=AXIS2_PLACEMENT_3D ( 'NONE', #105050, #73166, #39833 ) ;
#97906=DIRECTION ( 'NONE',  ( -0.6830127018922180770, -0.6830127018922204085, -0.2588190451025213501 ) ) ;
#97907=CARTESIAN_POINT ( 'NONE',  ( -75.18398860626899705, 28.73617430169839793, 5.000000000000000000 ) ) ;
#97908=CARTESIAN_POINT ( 'NONE',  ( -17.81601139373099940, 28.73617430169775133, 5.000000000000000000 ) ) ;
#97909=ORIENTED_EDGE ( 'NONE', *, *, #135193, .T. ) ;
#97913=ORIENTED_EDGE ( 'NONE', *, *, #17068, .T. ) ;
#97914=ORIENTED_EDGE ( 'NONE', *, *, #26858, .F. ) ;
#97916=ORIENTED_EDGE ( 'NONE', *, *, #125227, .F. ) ;
#97917=DIRECTION ( 'NONE',  ( -0.000000000000000000, 0.000000000000000000, 1.000000000000000000 ) ) ;
#97918=PLANE ( 'NONE',  #111089 ) ;
#97919=VECTOR ( 'NONE', #8405, 1000.000000000000000 ) ;
#97920=ORIENTED_EDGE ( 'NONE', *, *, #23391, .T. ) ;
#97921=CARTESIAN_POINT ( 'NONE',  ( -9.707106781186471522, -6.740707523384216415, 5.000000000000000000 ) ) ;
#97923=PLANE ( 'NONE',  #41782 ) ;
#97924=FACE_OUTER_BOUND ( 'NONE', #121076, .T. ) ;
#97925=ADVANCED_FACE ( 'NONE', ( #42884 ), #53755, .F. ) ;
#97926=ORIENTED_EDGE ( 'NONE', *, *, #28176, .F. ) ;
#97929=DIRECTION ( 'NONE',  ( 0.7071067811865487940, -0.7071067811865463515, 0.000000000000000000 ) ) ;
#97930=CARTESIAN_POINT ( 'NONE',  ( 25.49999999999982236, -1.592773361805348342, -6.492772025301288608 ) ) ;
#97931=DIRECTION ( 'NONE',  ( 0.7071067811865487940, 0.7071067811865463515, 0.000000000000000000 ) ) ;
#97934=CARTESIAN_POINT ( 'NONE',  ( 23.18753812416036908, -22.22500000000000142, 4.000000000000000000 ) ) ;
#97935=ORIENTED_EDGE ( 'NONE', *, *, #52200, .T. ) ;
#97936=ORIENTED_EDGE ( 'NONE', *, *, #90672, .T. ) ;
#97938=VERTEX_POINT ( 'NONE', #129867 ) ;
#97940=LINE ( 'NONE', #42870, #124308 ) ;
#97941=AXIS2_PLACEMENT_3D ( 'NONE', #81873, #12284, #59401 ) ;
#97942=LINE ( 'NONE', #78335, #52643 ) ;
#97943=FACE_OUTER_BOUND ( 'NONE', #138284, .T. ) ;
#97944=VECTOR ( 'NONE', #84848, 1000.000000000000000 ) ;
#97947=VECTOR ( 'NONE', #74300, 1000.000000000000114 ) ;
#97949=ADVANCED_FACE ( 'NONE', ( #29124 ), #52295, .F. ) ;
#97950=ORIENTED_EDGE ( 'NONE', *, *, #22063, .T. ) ;
#97951=ORIENTED_EDGE ( 'NONE', *, *, #112612, .T. ) ;
#97952=VECTOR ( 'NONE', #98887, 999.9999999999998863 ) ;
#97953=VECTOR ( 'NONE', #117605, 1000.000000000000000 ) ;
#97954=DIRECTION ( 'NONE',  ( -0.6830127018922181881, 0.6830127018922202975, -0.2588190451025214056 ) ) ;
#97955=LINE ( 'NONE', #75491, #59417 ) ;
#97956=CARTESIAN_POINT ( 'NONE',  ( -12.54133533107846432, 22.22500000000000142, -3.482007288379135979 ) ) ;
#97957=DIRECTION ( 'NONE',  ( 0.7071067811865487940, -0.7071067811865463515, 0.000000000000000000 ) ) ;
#97958=ORIENTED_EDGE ( 'NONE', *, *, #40865, .F. ) ;
#97961=CARTESIAN_POINT ( 'NONE',  ( 3.469446951953614189E-15, -13.44781430457069327, 5.000000000000000000 ) ) ;
#97962=EDGE_CURVE ( 'NONE', #131602, #18734, #142192, .T. ) ;
#97963=DIRECTION ( 'NONE',  ( 0.7071067811865487940, 0.7071067811865463515, -0.000000000000000000 ) ) ;
#97967=VECTOR ( 'NONE', #20479, 1000.000000000000000 ) ;
#97969=EDGE_LOOP ( 'NONE', ( #126943, #138611, #83331 ) ) ;
#97970=DIRECTION ( 'NONE',  ( -0.7071067811865487940, 0.7071067811865463515, 0.000000000000000000 ) ) ;
#97971=EDGE_LOOP ( 'NONE', ( #27344, #11684, #33577, #71780 ) ) ;
#97973=EDGE_LOOP ( 'NONE', ( #68010, #122601, #81932, #33481 ) ) ;
#97974=AXIS2_PLACEMENT_3D ( 'NONE', #34551, #3314, #124406 ) ;
#97975=LINE ( 'NONE', #74085, #130927 ) ;
#97977=ORIENTED_EDGE ( 'NONE', *, *, #116268, .F. ) ;
#97978=VECTOR ( 'NONE', #31530, 1000.000000000000000 ) ;
#97979=DIRECTION ( 'NONE',  ( -0.7071067811865487940, 0.7071067811865463515, -0.000000000000000000 ) ) ;
#97980=LINE ( 'NONE', #120394, #43626 ) ;
#97981=CARTESIAN_POINT ( 'NONE',  ( 6.707106781186496391, -3.740707523384244837, 5.000000000000000000 ) ) ;
#97982=VECTOR ( 'NONE', #50444, 1000.000000000000000 ) ;
#97983=FACE_BOUND ( 'NONE', #88609, .T. ) ;
#97984=EDGE_LOOP ( 'NONE', ( #19822, #40311, #95689, #5630 ) ) ;
#97985=FACE_OUTER_BOUND ( 'NONE', #120665, .T. ) ;
#97986=DIRECTION ( 'NONE',  ( 1.000000000000000000, 0.000000000000000000, 0.000000000000000000 ) ) ;
#97987=CARTESIAN_POINT ( 'NONE',  ( 36.48921356237310221, -27.52281430457080802, 5.000000000000000000 ) ) ;
#97989=VERTEX_POINT ( 'NONE', #87079 ) ;
#97990=ORIENTED_EDGE ( 'NONE', *, *, #138240, .F. ) ;
#97992=VECTOR ( 'NONE', #116050, 1000.000000000000000 ) ;
#97993=EDGE_CURVE ( 'NONE', #48713, #135328, #18961, .T. ) ;
#97995=VECTOR ( 'NONE', #56900, 999.9999999999998863 ) ;
#97996=VERTEX_POINT ( 'NONE', #31977 ) ;
#97998=PLANE ( 'NONE',  #134426 ) ;
#97999=EDGE_CURVE ( 'NONE', #116750, #54134, #18208, .T. ) ;
#98000=EDGE_LOOP ( 'NONE', ( #40078, #141539, #39941, #109402 ) ) ;
#98001=LINE ( 'NONE', #99387, #116758 ) ;
#98002=CARTESIAN_POINT ( 'NONE',  ( -18.29974487139159223, -27.71228299555219010, 4.000000000000000000 ) ) ;
#98003=VERTEX_POINT ( 'NONE', #7349 ) ;
#98004=ADVANCED_FACE ( 'NONE', ( #107393 ), #8742, .F. ) ;
#98005=CARTESIAN_POINT ( 'NONE',  ( 34.92499999999998295, 15.85612307739225280, 4.000000000000000000 ) ) ;
#98006=DIRECTION ( 'NONE',  ( -0.7071067811865487940, 0.7071067811865463515, -0.000000000000000000 ) ) ;
#98007=AXIS2_PLACEMENT_3D ( 'NONE', #120528, #76359, #36246 ) ;
#98008=EDGE_CURVE ( 'NONE', #95760, #113826, #97783, .T. ) ;
#98009=DIRECTION ( 'NONE',  ( 0.7071067811865487940, -0.7071067811865463515, 0.000000000000000000 ) ) ;
#98010=FACE_OUTER_BOUND ( 'NONE', #44158, .T. ) ;
#98011=DIRECTION ( 'NONE',  ( 0.3543493200069163240, -0.000000000000000000, 0.9351131265310288487 ) ) ;
#98012=DIRECTION ( 'NONE',  ( 0.7071067811865487940, -0.7071067811865463515, -0.000000000000000000 ) ) ;
#98013=PLANE ( 'NONE',  #132021 ) ;
#98015=VECTOR ( 'NONE', #17024, 1000.000000000000000 ) ;
#98016=EDGE_LOOP ( 'NONE', ( #110735, #15013, #136883, #103641 ) ) ;
#98017=ORIENTED_EDGE ( 'NONE', *, *, #110234, .T. ) ;
#98018=CARTESIAN_POINT ( 'NONE',  ( 33.81246187583924723, -22.22500000000000142, 4.000000000000000000 ) ) ;
#98019=LINE ( 'NONE', #43624, #60737 ) ;
#98021=ORIENTED_EDGE ( 'NONE', *, *, #80512, .F. ) ;
#98022=LINE ( 'NONE', #140114, #123030 ) ;
#98023=LINE ( 'NONE', #20433, #115042 ) ;
#98024=ADVANCED_FACE ( 'NONE', ( #142030 ), #53580, .F. ) ;
#98025=ADVANCED_FACE ( 'NONE', ( #76783 ), #99931, .F. ) ;
#98027=VECTOR ( 'NONE', #46828, 999.9999999999998863 ) ;
#98028=ORIENTED_EDGE ( 'NONE', *, *, #62976, .T. ) ;
#98029=CARTESIAN_POINT ( 'NONE',  ( 0.000000000000000000, 0.000000000000000000, 5.000000000000000000 ) ) ;
#98030=EDGE_CURVE ( 'NONE', #139938, #131028, #109371, .T. ) ;
#98033=VECTOR ( 'NONE', #140437, 1000.000000000000000 ) ;
#98034=DIRECTION ( 'NONE',  ( -0.000000000000000000, -0.3543493200069152693, 0.9351131265310292928 ) ) ;
#98037=CARTESIAN_POINT ( 'NONE',  ( -63.48921356237309510, -27.52281430457099631, 5.000000000000000000 ) ) ;
#98038=CARTESIAN_POINT ( 'NONE',  ( 14.99999999999990230, -0.2811185226894094558, -5.995736974527545726 ) ) ;
#98039=EDGE_CURVE ( 'NONE', #2079, #79854, #98298, .T. ) ;
#98040=CARTESIAN_POINT ( 'NONE',  ( 9.793339364578407924, 21.75929247661549937, 4.998822639870711626 ) ) ;
#98041=VERTEX_POINT ( 'NONE', #64440 ) ;
#98042=CARTESIAN_POINT ( 'NONE',  ( -32.99451991528749062, 28.92564299267960948, 4.000000000000000000 ) ) ;
#98043=VERTEX_POINT ( 'NONE', #74627 ) ;
#98044=CARTESIAN_POINT ( 'NONE',  ( -25.49999999999982236, -4.533600742197692490, 5.000000000000000000 ) ) ;
#98045=DIRECTION ( 'NONE',  ( -8.817971600062198362E-18, -0.3543493200069152693, 0.9351131265310292928 ) ) ;
#98046=LINE ( 'NONE', #87162, #139806 ) ;
#98047=VECTOR ( 'NONE', #20248, 1000.000000000000000 ) ;
#98049=CARTESIAN_POINT ( 'NONE',  ( 23.99451991528749062, 28.92564299267954908, 4.000000000000000000 ) ) ;
#98052=VECTOR ( 'NONE', #28512, 999.9999999999998863 ) ;
#98053=ORIENTED_EDGE ( 'NONE', *, *, #2673, .T. ) ;
#98054=CARTESIAN_POINT ( 'NONE',  ( -24.48921356237309510, -27.52281430457072631, 5.000000000000000000 ) ) ;
#98055=CARTESIAN_POINT ( 'NONE',  ( 21.18398860626899349, 28.73617430169802134, 5.000000000000000000 ) ) ;
#98056=ORIENTED_EDGE ( 'NONE', *, *, #37958, .T. ) ;
#98057=DIRECTION ( 'NONE',  ( -0.7071067811865486830, -0.7071067811865464625, -0.000000000000000000 ) ) ;
#98058=DIRECTION ( 'NONE',  ( 0.7071067811865486830, -0.7071067811865464625, -0.000000000000000000 ) ) ;
#98059=ORIENTED_EDGE ( 'NONE', *, *, #10048, .T. ) ;
#98060=VERTEX_POINT ( 'NONE', #120209 ) ;
#98061=DIRECTION ( 'NONE',  ( -0.3543493200069162685, -0.000000000000000000, -0.9351131265310288487 ) ) ;
#98062=LINE ( 'NONE', #10313, #76047 ) ;
#98063=VECTOR ( 'NONE', #64650, 1000.000000000000227 ) ;
#98064=ADVANCED_FACE ( 'NONE', ( #10053 ), #131854, .F. ) ;
#98067=FACE_OUTER_BOUND ( 'NONE', #16215, .T. ) ;
#98068=DIRECTION ( 'NONE',  ( -0.6830127018922181881, 0.6830127018922202975, -0.2588190451025214056 ) ) ;
#98069=ORIENTED_EDGE ( 'NONE', *, *, #138255, .T. ) ;
#98070=DIRECTION ( 'NONE',  ( -0.000000000000000000, -0.000000000000000000, 1.000000000000000000 ) ) ;
#98071=DIRECTION ( 'NONE',  ( 0.3543493200069162685, -0.000000000000000000, -0.9351131265310288487 ) ) ;
#98072=CARTESIAN_POINT ( 'NONE',  ( -14.99999999999990230, 7.559798855135676732, 4.979909187984716823 ) ) ;
#98073=CARTESIAN_POINT ( 'NONE',  ( -34.92500000000001137, 22.22500000000000142, 4.000000000000000000 ) ) ;
#98075=VECTOR ( 'NONE', #42249, 1000.000000000000000 ) ;
#98076=VERTEX_POINT ( 'NONE', #20196 ) ;
#98077=ORIENTED_EDGE ( 'NONE', *, *, #5232, .F. ) ;
#98078=DIRECTION ( 'NONE',  ( -0.7071067811865487940, 0.7071067811865463515, -0.000000000000000000 ) ) ;
#98079=VECTOR ( 'NONE', #62569, 999.9999999999998863 ) ;
#98080=ORIENTED_EDGE ( 'NONE', *, *, #5215, .T. ) ;
#98081=EDGE_CURVE ( 'NONE', #135356, #79591, #88357, .T. ) ;
#98083=VERTEX_POINT ( 'NONE', #8577 ) ;
#98084=CARTESIAN_POINT ( 'NONE',  ( 25.17183060077629264, 3.759292476615674783, 4.000000000000000000 ) ) ;
#98085=FACE_OUTER_BOUND ( 'NONE', #91633, .T. ) ;
#98086=VERTEX_POINT ( 'NONE', #99180 ) ;
#98087=CARTESIAN_POINT ( 'NONE',  ( 45.29974487139158867, -27.71228299555237840, 4.000000000000000000 ) ) ;
#98088=LINE ( 'NONE', #97331, #132234 ) ;
#98090=CARTESIAN_POINT ( 'NONE',  ( -33.70710678118629744, -15.74070752338412760, 5.000000000000000000 ) ) ;
#98091=PLANE ( 'NONE',  #58128 ) ;
#98092=DIRECTION ( 'NONE',  ( -0.7071067811865486830, -0.7071067811865464625, -0.000000000000000000 ) ) ;
#98093=EDGE_CURVE ( 'NONE', #76846, #77009, #44133, .T. ) ;
#98094=ORIENTED_EDGE ( 'NONE', *, *, #122647, .T. ) ;
#98095=CARTESIAN_POINT ( 'NONE',  ( -10.49999999999992539, -4.216083040037264418, -7.486842126848634038 ) ) ;
#98096=CARTESIAN_POINT ( 'NONE',  ( 17.51078643762690845, -27.52281430457043143, 5.000000000000000000 ) ) ;
#98097=CARTESIAN_POINT ( 'NONE',  ( -15.48921356237309510, -27.52281430457066236, 5.000000000000000000 ) ) ;
#98099=FACE_OUTER_BOUND ( 'NONE', #50800, .T. ) ;
#98100=DIRECTION ( 'NONE',  ( -0.6830127018922181881, 0.6830127018922202975, -0.2588190451025214056 ) ) ;
#98101=PLANE ( 'NONE',  #24980 ) ;
#98102=AXIS2_PLACEMENT_3D ( 'NONE', #91738, #100497, #44728 ) ;
#98104=VECTOR ( 'NONE', #86963, 1000.000000000000000 ) ;
#98105=CARTESIAN_POINT ( 'NONE',  ( 29.99451991528749417, 28.92564299267958816, 4.000000000000000000 ) ) ;
#98107=ORIENTED_EDGE ( 'NONE', *, *, #3894, .F. ) ;
#98109=CARTESIAN_POINT ( 'NONE',  ( 27.29974487139158512, -27.71228299555225405, 4.000000000000000000 ) ) ;
#98110=CARTESIAN_POINT ( 'NONE',  ( -29.38161509397986038, -2.240707523384260824, 13.37739548510246124 ) ) ;
#98112=DIRECTION ( 'NONE',  ( 0.3543493200069162685, -0.000000000000000000, -0.9351131265310288487 ) ) ;
#98113=VERTEX_POINT ( 'NONE', #21661 ) ;
#98114=LINE ( 'NONE', #143038, #36311 ) ;
#98115=CARTESIAN_POINT ( 'NONE',  ( -25.22850677138649189, 20.25929247661551003, 7.808871592221711566 ) ) ;
#98118=ORIENTED_EDGE ( 'NONE', *, *, #96630, .F. ) ;
#98119=CARTESIAN_POINT ( 'NONE',  ( -34.49999999999975131, -4.535744391599457082, 4.994342998332168548 ) ) ;
#98121=ORIENTED_EDGE ( 'NONE', *, *, #68574, .T. ) ;
#98122=AXIS2_PLACEMENT_3D ( 'NONE', #128539, #18300, #137989 ) ;
#98123=CARTESIAN_POINT ( 'NONE',  ( 54.18398860626899705, 28.73617430169825226, 5.000000000000000000 ) ) ;
#98125=DIRECTION ( 'NONE',  ( -0.7071067811865486830, -0.7071067811865464625, 0.000000000000000000 ) ) ;
#98126=CARTESIAN_POINT ( 'NONE',  ( 20.99451991528748707, 28.92564299267952777, 4.000000000000000000 ) ) ;
#98127=ORIENTED_EDGE ( 'NONE', *, *, #11279, .F. ) ;
#98128=ADVANCED_FACE ( 'NONE', ( #86205 ), #75337, .F. ) ;
#98129=DIRECTION ( 'NONE',  ( 0.6830127018922180770, -0.6830127018922204085, -0.2588190451025213501 ) ) ;
#98130=DIRECTION ( 'NONE',  ( -0.7071067811865486830, 0.7071067811865464625, 0.000000000000000000 ) ) ;
#98131=PLANE ( 'NONE',  #31421 ) ;
#98132=ORIENTED_EDGE ( 'NONE', *, *, #46303, .F. ) ;
#98134=EDGE_CURVE ( 'NONE', #71727, #48744, #108623, .T. ) ;
#98135=LINE ( 'NONE', #43050, #71728 ) ;
#98136=LINE ( 'NONE', #53181, #29257 ) ;
#98139=CARTESIAN_POINT ( 'NONE',  ( -13.49999999999990408, 19.39370406404965763, 1.459788787078232897 ) ) ;
#98140=CARTESIAN_POINT ( 'NONE',  ( 30.18398860626900060, 28.73617430169808173, 5.000000000000000000 ) ) ;
#98141=ORIENTED_EDGE ( 'NONE', *, *, #136752, .T. ) ;
#98142=VECTOR ( 'NONE', #36509, 1000.000000000000227 ) ;
#98143=CARTESIAN_POINT ( 'NONE',  ( -11.99999999999991296, 14.96639925780211478, 5.000000000000000000 ) ) ;
#98145=PLANE ( 'NONE',  #60308 ) ;
#98147=ORIENTED_EDGE ( 'NONE', *, *, #25210, .T. ) ;
#98148=ORIENTED_EDGE ( 'NONE', *, *, #61510, .F. ) ;
#98149=DIRECTION ( 'NONE',  ( -0.7071067811865486830, 0.7071067811865464625, 0.000000000000000000 ) ) ;
#98150=PLANE ( 'NONE',  #46891 ) ;
#98151=VERTEX_POINT ( 'NONE', #143425 ) ;
#98152=EDGE_CURVE ( 'NONE', #44496, #44686, #132596, .T. ) ;
#98154=ORIENTED_EDGE ( 'NONE', *, *, #40918, .T. ) ;
#98155=CARTESIAN_POINT ( 'NONE',  ( 24.18398860626899705, 28.73617430169804265, 5.000000000000000000 ) ) ;
#98156=ORIENTED_EDGE ( 'NONE', *, *, #45813, .F. ) ;
#98157=DIRECTION ( 'NONE',  ( 0.7071067811865486830, -0.7071067811865464625, -0.000000000000000000 ) ) ;
#98158=CARTESIAN_POINT ( 'NONE',  ( 10.49999999999992539, 6.431123077392117082, 4.000000000000000000 ) ) ;
#98160=FACE_BOUND ( 'NONE', #76946, .T. ) ;
#98161=CARTESIAN_POINT ( 'NONE',  ( -34.42500000000001137, -21.72500000000000142, 4.500000000000000888 ) ) ;
#98162=LINE ( 'NONE', #76421, #72115 ) ;
#98165=ORIENTED_EDGE ( 'NONE', *, *, #122164, .T. ) ;
#98166=VECTOR ( 'NONE', #131529, 999.9999999999998863 ) ;
#98167=CARTESIAN_POINT ( 'NONE',  ( 31.74845587132405811, -11.24070752338416135, 10.39518518046001994 ) ) ;
#98168=ORIENTED_EDGE ( 'NONE', *, *, #107260, .T. ) ;
#98169=VECTOR ( 'NONE', #129273, 1000.000000000000000 ) ;
#98170=EDGE_CURVE ( 'NONE', #89800, #56401, #66599, .T. ) ;
#98171=VERTEX_POINT ( 'NONE', #24499 ) ;
#98173=VERTEX_POINT ( 'NONE', #113647 ) ;
#98174=PLANE ( 'NONE',  #81443 ) ;
#98176=VERTEX_POINT ( 'NONE', #45584 ) ;
#98177=DIRECTION ( 'NONE',  ( -0.000000000000000000, 0.000000000000000000, 1.000000000000000000 ) ) ;
#98178=EDGE_CURVE ( 'NONE', #122443, #81871, #47731, .T. ) ;
#98179=ADVANCED_FACE ( 'NONE', ( #36806 ), #34685, .F. ) ;
#98181=LINE ( 'NONE', #141691, #36792 ) ;
#98182=FACE_OUTER_BOUND ( 'NONE', #101044, .T. ) ;
#98183=VECTOR ( 'NONE', #121204, 1000.000000000000227 ) ;
#98184=CARTESIAN_POINT ( 'NONE',  ( 28.37176554955598462, -8.240707523384193323, 11.38925528200746129 ) ) ;
#98185=PLANE ( 'NONE',  #5292 ) ;
#98187=ORIENTED_EDGE ( 'NONE', *, *, #53650, .T. ) ;
#98188=ORIENTED_EDGE ( 'NONE', *, *, #30583, .F. ) ;
#98190=DIRECTION ( 'NONE',  ( 0.6830127018922180770, -0.6830127018922204085, -0.2588190451025213501 ) ) ;
#98191=AXIS2_PLACEMENT_3D ( 'NONE', #40825, #77047, #107495 ) ;
#98193=VERTEX_POINT ( 'NONE', #134734 ) ;
#98194=LINE ( 'NONE', #43811, #56852 ) ;
#98195=EDGE_CURVE ( 'NONE', #119529, #120251, #12193, .T. ) ;
#98197=EDGE_CURVE ( 'NONE', #50863, #103304, #36120, .T. ) ;
#98199=EDGE_LOOP ( 'NONE', ( #123979, #35100, #93289, #119798 ) ) ;
#98200=CARTESIAN_POINT ( 'NONE',  ( -20.90332935812582349, -2.240707523384260824, 15.26439735382747642 ) ) ;
#98201=VECTOR ( 'NONE', #12576, 1000.000000000000000 ) ;
#98202=LINE ( 'NONE', #77876, #74801 ) ;
#98203=VECTOR ( 'NONE', #122810, 1000.000000000000227 ) ;
#98206=ADVANCED_FACE ( 'NONE', ( #136116 ), #68755, .T. ) ;
#98207=ORIENTED_EDGE ( 'NONE', *, *, #136004, .T. ) ;
#98208=VERTEX_POINT ( 'NONE', #101349 ) ;
#98209=FACE_OUTER_BOUND ( 'NONE', #101729, .T. ) ;
#98210=CARTESIAN_POINT ( 'NONE',  ( -36.18398860626899705, 28.73617430169812437, 5.000000000000000000 ) ) ;
#98211=EDGE_CURVE ( 'NONE', #76142, #132249, #68068, .T. ) ;
#98212=LINE ( 'NONE', #22049, #16945 ) ;
#98213=ORIENTED_EDGE ( 'NONE', *, *, #55183, .T. ) ;
#98214=ORIENTED_EDGE ( 'NONE', *, *, #91810, .F. ) ;
#98215=DIRECTION ( 'NONE',  ( -0.7071067811865486830, -0.7071067811865464625, 0.000000000000000000 ) ) ;
#98217=PLANE ( 'NONE',  #86502 ) ;
#98218=ORIENTED_EDGE ( 'NONE', *, *, #141379, .T. ) ;
#98219=DIRECTION ( 'NONE',  ( 0.7071067811865487940, 0.7071067811865463515, 0.000000000000000000 ) ) ;
#98220=ORIENTED_EDGE ( 'NONE', *, *, #109766, .T. ) ;
#98221=VERTEX_POINT ( 'NONE', #47042 ) ;
#98222=ORIENTED_EDGE ( 'NONE', *, *, #111138, .F. ) ;
#98224=CARTESIAN_POINT ( 'NONE',  ( 34.75611968250419181, 11.81293425470726710, 4.955485411084880276 ) ) ;
#98225=AXIS2_PLACEMENT_3D ( 'NONE', #67402, #140139, #23115 ) ;
#98226=EDGE_CURVE ( 'NONE', #22380, #27557, #70209, .T. ) ;
#98227=DIRECTION ( 'NONE',  ( 0.6830127018922181881, 0.6830127018922202975, -0.2588190451025214056 ) ) ;
#98228=FACE_OUTER_BOUND ( 'NONE', #33770, .T. ) ;
#98229=DIRECTION ( 'NONE',  ( -0.7071067811865487940, 0.7071067811865463515, -0.000000000000000000 ) ) ;
#98230=CARTESIAN_POINT ( 'NONE',  ( 10.49999999999992539, -16.53360074219757081, 5.000000000000000000 ) ) ;
#98231=CARTESIAN_POINT ( 'NONE',  ( -11.29289321881337393, 20.25929247661551003, 5.000000000000000000 ) ) ;
#98233=DIRECTION ( 'NONE',  ( 0.7071067811865487940, -0.7071067811865463515, 0.000000000000000000 ) ) ;
#98234=EDGE_CURVE ( 'NONE', #85558, #132912, #112242, .T. ) ;
#98235=ORIENTED_EDGE ( 'NONE', *, *, #124054, .T. ) ;
#98236=ADVANCED_FACE ( 'NONE', ( #13605 ), #125250, .T. ) ;
#98237=CARTESIAN_POINT ( 'NONE',  ( -33.79289321881321939, -11.24070752338416668, 5.000000000000000000 ) ) ;
#98238=EDGE_CURVE ( 'NONE', #86975, #39389, #114369, .T. ) ;
#98239=DIRECTION ( 'NONE',  ( -0.000000000000000000, 0.000000000000000000, 1.000000000000000000 ) ) ;
#98240=EDGE_LOOP ( 'NONE', ( #42360, #70776, #47448, #25750 ) ) ;
#98241=DIRECTION ( 'NONE',  ( 0.7071067811865487940, 0.7071067811865463515, 0.000000000000000000 ) ) ;
#98245=ORIENTED_EDGE ( 'NONE', *, *, #78454, .T. ) ;
#98247=CARTESIAN_POINT ( 'NONE',  ( -20.20710678118640402, -11.24070752338416312, 5.000000000000000000 ) ) ;
#98250=ADVANCED_FACE ( 'NONE', ( #14345 ), #133293, .F. ) ;
#98251=PLANE ( 'NONE',  #103790 ) ;
#98254=DIRECTION ( 'NONE',  ( -0.000000000000000000, -0.3543493200069152693, 0.9351131265310292928 ) ) ;
#98258=ORIENTED_EDGE ( 'NONE', *, *, #71358, .F. ) ;
#98259=CARTESIAN_POINT ( 'NONE',  ( -17.72082203615853047, 8.995094813919580545, 4.338987337627234098 ) ) ;
#98260=VERTEX_POINT ( 'NONE', #23801 ) ;
#98261=DIRECTION ( 'NONE',  ( -0.7071067811865486830, -0.7071067811865464625, 0.000000000000000000 ) ) ;
#98262=CARTESIAN_POINT ( 'NONE',  ( -26.99999999999981526, 19.93112307739197675, 4.000000000000000000 ) ) ;
#98264=PLANE ( 'NONE',  #18271 ) ;
#98265=DIRECTION ( 'NONE',  ( -0.3543493200069162685, -0.000000000000000000, -0.9351131265310288487 ) ) ;
#98266=EDGE_LOOP ( 'NONE', ( #107119, #23974, #31720, #25769 ) ) ;
#98268=CARTESIAN_POINT ( 'NONE',  ( 30.75860074219774631, 21.72500000000000142, 5.000000000000000000 ) ) ;
#98269=CARTESIAN_POINT ( 'NONE',  ( -11.20710678118646619, -2.240707523384255939, 5.000000000000000000 ) ) ;
#98270=ORIENTED_EDGE ( 'NONE', *, *, #70258, .T. ) ;
#98271=EDGE_LOOP ( 'NONE', ( #34580, #27014, #11842, #112751 ) ) ;
#98273=DIRECTION ( 'NONE',  ( 0.7071067811865486830, -0.7071067811865464625, -0.000000000000000000 ) ) ;
#98275=VECTOR ( 'NONE', #32038, 1000.000000000000000 ) ;
#98276=FACE_OUTER_BOUND ( 'NONE', #100263, .T. ) ;
#98277=LINE ( 'NONE', #43188, #64231 ) ;
#98279=CARTESIAN_POINT ( 'NONE',  ( -63.18398860626900415, 28.73617430169831621, 5.000000000000000000 ) ) ;
#98281=CARTESIAN_POINT ( 'NONE',  ( 34.92499999999998295, -10.29806943317891310, 4.500000000000000888 ) ) ;
#98282=ORIENTED_EDGE ( 'NONE', *, *, #23042, .F. ) ;
#98284=CARTESIAN_POINT ( 'NONE',  ( -20.24139925780189841, 21.72500000000000853, 5.000000000000000000 ) ) ;
#98286=EDGE_CURVE ( 'NONE', #139251, #114615, #56476, .T. ) ;
#98290=( BOUNDED_CURVE ( )  B_SPLINE_CURVE ( 3, ( #138267, #127378, #50541, #39690 ),
 .UNSPECIFIED., .F., .F. ) 
 B_SPLINE_CURVE_WITH_KNOTS ( ( 4, 4 ),
 ( 2.001653308786170982, 3.503810798801451742 ),
 .UNSPECIFIED. ) 
 CURVE ( )  GEOMETRIC_REPRESENTATION_ITEM ( )  RATIONAL_B_SPLINE_CURVE ( ( 1.000000000000000000, 0.8206354192515243895, 0.8206354192515243895, 1.000000000000000000 ) ) 
 REPRESENTATION_ITEM ( '' )  );
#98291=DIRECTION ( 'NONE',  ( -0.7071067811865487940, 0.7071067811865463515, -0.000000000000000000 ) ) ;
#98292=ORIENTED_EDGE ( 'NONE', *, *, #120707, .T. ) ;
#98293=VECTOR ( 'NONE', #81128, 999.9999999999998863 ) ;
#98295=CARTESIAN_POINT ( 'NONE',  ( 0.000000000000000000, 0.000000000000000000, 5.000000000000000000 ) ) ;
#98297=PLANE ( 'NONE',  #51249 ) ;
#98298=( BOUNDED_CURVE ( )  B_SPLINE_CURVE ( 3, ( #77492, #118815, #54316, #130432 ),
 .UNSPECIFIED., .F., .T. ) 
 B_SPLINE_CURVE_WITH_KNOTS ( ( 4, 4 ),
 ( 1.208578181583235267, 1.359146454359470901 ),
 .UNSPECIFIED. ) 
 CURVE ( )  GEOMETRIC_REPRESENTATION_ITEM ( )  RATIONAL_B_SPLINE_CURVE ( ( 1.000000000000000000, 0.9981116584018945304, 0.9981116584018945304, 1.000000000000000000 ) ) 
 REPRESENTATION_ITEM ( '' )  );
#98299=DIRECTION ( 'NONE',  ( -0.7071067811865486830, -0.7071067811865464625, 0.000000000000000000 ) ) ;
#98300=DIRECTION ( 'NONE',  ( -0.7071067811865486830, 0.7071067811865464625, 0.000000000000000000 ) ) ;
#98301=EDGE_CURVE ( 'NONE', #88210, #129741, #100656, .T. ) ;
#98302=CARTESIAN_POINT ( 'NONE',  ( -75.48921356237309510, -27.52281430457107803, 5.000000000000000000 ) ) ;
#98303=CARTESIAN_POINT ( 'NONE',  ( 28.82816939922332722, -8.240707523384196875, 4.000000000000000000 ) ) ;
#98304=ORIENTED_EDGE ( 'NONE', *, *, #101514, .T. ) ;
#98305=ADVANCED_FACE ( 'NONE', ( #12898 ), #102800, .F. ) ;
#98307=DIRECTION ( 'NONE',  ( 0.7071067811865487940, 0.7071067811865463515, 0.000000000000000000 ) ) ;
#98308=FACE_OUTER_BOUND ( 'NONE', #119269, .T. ) ;
#98309=FACE_OUTER_BOUND ( 'NONE', #21867, .T. ) ;
#98310=VECTOR ( 'NONE', #139955, 1000.000000000000000 ) ;
#98311=ADVANCED_FACE ( 'NONE', ( #70893 ), #126655, .F. ) ;
#98312=ORIENTED_EDGE ( 'NONE', *, *, #24189, .T. ) ;
#98313=VERTEX_POINT ( 'NONE', #81781 ) ;
#98316=VECTOR ( 'NONE', #53664, 1000.000000000000000 ) ;
#98317=EDGE_LOOP ( 'NONE', ( #24421, #29508, #109791, #131136 ) ) ;
#98318=AXIS2_PLACEMENT_3D ( 'NONE', #123856, #47742, #136129 ) ;
#98319=EDGE_CURVE ( 'NONE', #4377, #115184, #30021, .T. ) ;
#98320=DIRECTION ( 'NONE',  ( -0.7071067811865486830, -0.7071067811865464625, 0.000000000000000000 ) ) ;
#98321=CARTESIAN_POINT ( 'NONE',  ( -2.999999999999981792, 10.21212019023809070, -2.019456568337790969 ) ) ;
#98324=ORIENTED_EDGE ( 'NONE', *, *, #103968, .T. ) ;
#98325=ORIENTED_EDGE ( 'NONE', *, *, #36614, .T. ) ;
#98326=LINE ( 'NONE', #88888, #65435 ) ;
#98327=LINE ( 'NONE', #87452, #125386 ) ;
#98328=ADVANCED_FACE ( 'NONE', ( #119865 ), #4842, .F. ) ;
#98329=AXIS2_PLACEMENT_3D ( 'NONE', #34519, #78747, #46886 ) ;
#98330=VERTEX_POINT ( 'NONE', #125977 ) ;
#98331=DIRECTION ( 'NONE',  ( -0.000000000000000000, 0.3543493200069153248, 0.9351131265310292928 ) ) ;
#98332=LINE ( 'NONE', #102620, #85032 ) ;
#98333=FACE_OUTER_BOUND ( 'NONE', #88370, .T. ) ;
#98334=EDGE_CURVE ( 'NONE', #15605, #90375, #109004, .T. ) ;
#98336=FACE_BOUND ( 'NONE', #134023, .T. ) ;
#98338=DIRECTION ( 'NONE',  ( -0.7071067811865486830, 0.7071067811865464625, 0.000000000000000000 ) ) ;
#98340=EDGE_CURVE ( 'NONE', #82317, #73248, #113093, .T. ) ;
#98344=ORIENTED_EDGE ( 'NONE', *, *, #12104, .F. ) ;
#98345=ORIENTED_EDGE ( 'NONE', *, *, #69492, .T. ) ;
#98347=VERTEX_POINT ( 'NONE', #86579 ) ;
#98348=ORIENTED_EDGE ( 'NONE', *, *, #46889, .F. ) ;
#98353=EDGE_CURVE ( 'NONE', #133319, #34241, #107589, .T. ) ;
#98354=ADVANCED_FACE ( 'NONE', ( #85838 ), #85126, .F. ) ;
#98355=DIRECTION ( 'NONE',  ( -0.000000000000000000, 0.000000000000000000, 1.000000000000000000 ) ) ;
#98359=PLANE ( 'NONE',  #71234 ) ;
#98360=DIRECTION ( 'NONE',  ( 0.7071067811865487940, 0.7071067811865463515, -0.000000000000000000 ) ) ;
#98361=DIRECTION ( 'NONE',  ( -0.7071067811865487940, 0.7071067811865463515, -0.000000000000000000 ) ) ;
#98363=ORIENTED_EDGE ( 'NONE', *, *, #9348, .F. ) ;
#98364=ADVANCED_FACE ( 'NONE', ( #37544 ), #8247, .F. ) ;
#98365=DIRECTION ( 'NONE',  ( -0.6830127018922181881, 0.6830127018922202975, -0.2588190451025214056 ) ) ;
#98366=CARTESIAN_POINT ( 'NONE',  ( -18.49816348513945385, -17.24070752338411339, 8.407044977365265126 ) ) ;
#98367=ORIENTED_EDGE ( 'NONE', *, *, #102207, .T. ) ;
#98368=ORIENTED_EDGE ( 'NONE', *, *, #134931, .T. ) ;
#98369=EDGE_CURVE ( 'NONE', #103418, #12595, #49142, .T. ) ;
#98370=ORIENTED_EDGE ( 'NONE', *, *, #136468, .T. ) ;
#98374=VECTOR ( 'NONE', #113610, 999.9999999999998863 ) ;
#98375=DIRECTION ( 'NONE',  ( 0.7071067811865487940, -0.7071067811865463515, 0.000000000000000000 ) ) ;
#98377=DIRECTION ( 'NONE',  ( -0.000000000000000000, -0.3543493200069152693, 0.9351131265310292928 ) ) ;
#98378=EDGE_CURVE ( 'NONE', #133903, #98841, #96681, .T. ) ;
#98379=AXIS2_PLACEMENT_3D ( 'NONE', #38225, #104894, #48374 ) ;
#98380=LINE ( 'NONE', #109239, #53525 ) ;
#98381=EDGE_LOOP ( 'NONE', ( #95838, #105850, #16330, #48378 ) ) ;
#98384=DIRECTION ( 'NONE',  ( 0.7071067811865487940, 0.7071067811865463515, 0.000000000000000000 ) ) ;
#98385=CARTESIAN_POINT ( 'NONE',  ( -19.49999999999985789, -14.94781430457067906, 5.000000000000000000 ) ) ;
#98386=DIRECTION ( 'NONE',  ( 0.7071067811865487940, 0.7071067811865463515, -0.000000000000000000 ) ) ;
#98387=ORIENTED_EDGE ( 'NONE', *, *, #52942, .T. ) ;
#98388=DIRECTION ( 'NONE',  ( -0.7071067811865487940, 0.7071067811865463515, -0.000000000000000000 ) ) ;
#98390=ORIENTED_EDGE ( 'NONE', *, *, #142541, .F. ) ;
#98391=EDGE_LOOP ( 'NONE', ( #108138, #128372, #102822, #84687 ) ) ;
#98394=EDGE_LOOP ( 'NONE', ( #31689, #73127, #100386, #89025 ) ) ;
#98396=FACE_OUTER_BOUND ( 'NONE', #11797, .T. ) ;
#98398=CARTESIAN_POINT ( 'NONE',  ( 2.999999999999981792, -0.03360074219773551141, 5.000000000000000000 ) ) ;
#98399=ORIENTED_EDGE ( 'NONE', *, *, #25368, .T. ) ;
#98400=VECTOR ( 'NONE', #38035, 1000.000000000000000 ) ;
#98401=ADVANCED_FACE ( 'NONE', ( #7549 ), #40923, .F. ) ;
#98402=AXIS2_PLACEMENT_3D ( 'NONE', #116384, #117077, #126531 ) ;
#98404=DIRECTION ( 'NONE',  ( 0.7071067811865487940, -0.7071067811865463515, 0.000000000000000000 ) ) ;
#98406=DIRECTION ( 'NONE',  ( 0.7071067811865487940, 0.7071067811865463515, 0.000000000000000000 ) ) ;
#98407=AXIS2_PLACEMENT_3D ( 'NONE', #109552, #10230, #134175 ) ;
#98409=ORIENTED_EDGE ( 'NONE', *, *, #2026, .F. ) ;
#98410=ORIENTED_EDGE ( 'NONE', *, *, #134186, .T. ) ;
#98411=EDGE_LOOP ( 'NONE', ( #11361, #33234, #61030, #36679 ) ) ;
#98412=DIRECTION ( 'NONE',  ( -0.6830127018922181881, 0.6830127018922202975, -0.2588190451025214056 ) ) ;
#98413=CARTESIAN_POINT ( 'NONE',  ( -28.49999999999980460, -7.420205493532925800, -2.617629953481318772 ) ) ;
#98414=CARTESIAN_POINT ( 'NONE',  ( -63.18398860626900415, 28.73617430169831621, 5.000000000000000000 ) ) ;
#98417=CARTESIAN_POINT ( 'NONE',  ( -30.18398860626900060, 28.73617430169808173, 5.000000000000000000 ) ) ;
#98418=LINE ( 'NONE', #143339, #2567 ) ;
#98419=ORIENTED_EDGE ( 'NONE', *, *, #55785, .F. ) ;
#98420=FACE_OUTER_BOUND ( 'NONE', #1215, .T. ) ;
#98421=ORIENTED_EDGE ( 'NONE', *, *, #124552, .T. ) ;
#98422=DIRECTION ( 'NONE',  ( -0.000000000000000000, 0.3543493200069153248, 0.9351131265310292928 ) ) ;
#98423=VERTEX_POINT ( 'NONE', #63421 ) ;
#98424=CARTESIAN_POINT ( 'NONE',  ( -7.828169399223474656, -5.240707523384230626, 4.000000000000000000 ) ) ;
#98425=VERTEX_POINT ( 'NONE', #140926 ) ;
#98426=DIRECTION ( 'NONE',  ( 0.6830127018922180770, -0.6830127018922204085, -0.2588190451025213501 ) ) ;
#98427=ORIENTED_EDGE ( 'NONE', *, *, #4928, .F. ) ;
#98428=CARTESIAN_POINT ( 'NONE',  ( -9.792893218813384593, 18.75929247661552779, 5.000000000000000000 ) ) ;
#98432=ORIENTED_EDGE ( 'NONE', *, *, #76437, .T. ) ;
#98433=CARTESIAN_POINT ( 'NONE',  ( 34.92499999999998295, -18.18334561358936341, 4.500000000000000888 ) ) ;
#98435=FACE_OUTER_BOUND ( 'NONE', #107566, .T. ) ;
#98438=CARTESIAN_POINT ( 'NONE',  ( -32.99999999999977263, 7.588810512006185505, -3.013526669885150611 ) ) ;
#98439=DIRECTION ( 'NONE',  ( 0.7071067811865486830, -0.7071067811865464625, -0.000000000000000000 ) ) ;
#98443=DIRECTION ( 'NONE',  ( -0.7071067811865486830, -0.7071067811865464625, 0.000000000000000000 ) ) ;
#98446=DIRECTION ( 'NONE',  ( -0.3543493200069162685, -0.000000000000000000, -0.9351131265310288487 ) ) ;
#98447=ORIENTED_EDGE ( 'NONE', *, *, #58949, .F. ) ;
#98448=CARTESIAN_POINT ( 'NONE',  ( 23.99999999999984013, -0.4125381241607464222, 4.000000000000000000 ) ) ;
#98451=DIRECTION ( 'NONE',  ( -0.7071067811865487940, 0.7071067811865463515, -0.000000000000000000 ) ) ;
#98452=CARTESIAN_POINT ( 'NONE',  ( -23.16347128873436745, 15.75929247661555976, 9.299976744542865603 ) ) ;
#98453=EDGE_CURVE ( 'NONE', #133772, #3598, #130076, .T. ) ;
#98455=ADVANCED_FACE ( 'NONE', ( #53204 ), #31475, .F. ) ;
#98456=EDGE_CURVE ( 'NONE', #50067, #142844, #11100, .T. ) ;
#98457=FACE_OUTER_BOUND ( 'NONE', #66569, .T. ) ;
#98458=FACE_OUTER_BOUND ( 'NONE', #28625, .T. ) ;
#98459=ORIENTED_EDGE ( 'NONE', *, *, #81574, .F. ) ;
#98460=CARTESIAN_POINT ( 'NONE',  ( 0.000000000000000000, 0.000000000000000000, 5.000000000000000000 ) ) ;
#98462=DIRECTION ( 'NONE',  ( -0.000000000000000000, 0.3543493200069153248, 0.9351131265310292928 ) ) ;
#98463=DIRECTION ( 'NONE',  ( -0.7071067811865486830, 0.7071067811865464625, 0.000000000000000000 ) ) ;
#98464=PLANE ( 'NONE',  #51536 ) ;
#98466=ORIENTED_EDGE ( 'NONE', *, *, #5241, .F. ) ;
#98467=EDGE_CURVE ( 'NONE', #86945, #115943, #142387, .T. ) ;
#98468=AXIS2_PLACEMENT_3D ( 'NONE', #11245, #86720, #120746 ) ;
#98469=ORIENTED_EDGE ( 'NONE', *, *, #72183, .T. ) ;
#98470=ORIENTED_EDGE ( 'NONE', *, *, #80634, .T. ) ;
#98472=VERTEX_POINT ( 'NONE', #23434 ) ;
#98473=VECTOR ( 'NONE', #127926, 999.9999999999998863 ) ;
#98474=EDGE_CURVE ( 'NONE', #101323, #46695, #43774, .T. ) ;
#98476=FACE_OUTER_BOUND ( 'NONE', #61943, .T. ) ;
#98478=LINE ( 'NONE', #120190, #60697 ) ;
#98480=ADVANCED_FACE ( 'NONE', ( #224 ), #56836, .F. ) ;
#98482=VECTOR ( 'NONE', #120310, 1000.000000000000227 ) ;
#98483=ORIENTED_EDGE ( 'NONE', *, *, #116830, .T. ) ;
#98484=CARTESIAN_POINT ( 'NONE',  ( -7.828169399223476432, 15.75929247661555976, 4.000000000000000000 ) ) ;
#98485=CARTESIAN_POINT ( 'NONE',  ( 36.29974487139159578, -27.71228299555231445, 4.000000000000000000 ) ) ;
#98486=ORIENTED_EDGE ( 'NONE', *, *, #68771, .T. ) ;
#98487=VERTEX_POINT ( 'NONE', #66252 ) ;
#98488=VERTEX_POINT ( 'NONE', #132956 ) ;
#98489=CARTESIAN_POINT ( 'NONE',  ( -17.99999999999987210, -21.41253812416053748, 4.000000000000000000 ) ) ;
#98490=CARTESIAN_POINT ( 'NONE',  ( -5.510786437626906675, -27.52281430457051314, 5.000000000000000000 ) ) ;
#98491=DIRECTION ( 'NONE',  ( -0.7071067811865487940, 0.7071067811865463515, -0.000000000000000000 ) ) ;
#98492=ADVANCED_FACE ( 'NONE', ( #87281 ), #123508, .F. ) ;
#98493=CARTESIAN_POINT ( 'NONE',  ( 42.18398860626899705, 28.73617430169816700, 5.000000000000000000 ) ) ;
#98495=CARTESIAN_POINT ( 'NONE',  ( -12.29974487139158512, -27.71228299555214747, 4.000000000000000000 ) ) ;
#98496=( NAMED_UNIT ( * ) SI_UNIT ( $, .STERADIAN. ) SOLID_ANGLE_UNIT ( ) );
#98497=VECTOR ( 'NONE', #36942, 1000.000000000000000 ) ;
#98498=VERTEX_POINT ( 'NONE', #55376 ) ;
#98499=VECTOR ( 'NONE', #139565, 1000.000000000000000 ) ;
#98500=ORIENTED_EDGE ( 'NONE', *, *, #47505, .F. ) ;
#98502=ORIENTED_EDGE ( 'NONE', *, *, #103550, .T. ) ;
#98503=ORIENTED_EDGE ( 'NONE', *, *, #20749, .F. ) ;
#98504=EDGE_CURVE ( 'NONE', #41140, #15309, #32930, .T. ) ;
#98505=AXIS2_PLACEMENT_3D ( 'NONE', #41733, #7653, #121420 ) ;
#98506=ADVANCED_FACE ( 'NONE', ( #33636 ), #32183, .F. ) ;
#98507=CARTESIAN_POINT ( 'NONE',  ( -1.500000000000001332, 22.08746187583903975, 4.000000000000000000 ) ) ;
#98508=ORIENTED_EDGE ( 'NONE', *, *, #114734, .F. ) ;
#98509=LINE ( 'NONE', #119513, #57628 ) ;
#98510=CARTESIAN_POINT ( 'NONE',  ( -30.48921356237309510, -27.52281430457076894, 5.000000000000000000 ) ) ;
#98511=EDGE_CURVE ( 'NONE', #106471, #126064, #111137, .T. ) ;
#98512=DIRECTION ( 'NONE',  ( 0.7071067811865487940, 0.7071067811865463515, 0.000000000000000000 ) ) ;
#98513=DIRECTION ( 'NONE',  ( -0.7071067811865486830, -0.7071067811865464625, -0.000000000000000000 ) ) ;
#98516=EDGE_CURVE ( 'NONE', #93730, #5674, #76418, .T. ) ;
#98517=DIRECTION ( 'NONE',  ( -0.3543493200069163240, 0.000000000000000000, -0.9351131265310288487 ) ) ;
#98518=ORIENTED_EDGE ( 'NONE', *, *, #53407, .F. ) ;
#98519=LINE ( 'NONE', #8602, #136051 ) ;
#98520=ORIENTED_EDGE ( 'NONE', *, *, #138106, .F. ) ;
#98521=DIRECTION ( 'NONE',  ( 0.6830127018922180770, -0.6830127018922204085, -0.2588190451025213501 ) ) ;
#98522=ORIENTED_EDGE ( 'NONE', *, *, #123365, .F. ) ;
#98523=DIRECTION ( 'NONE',  ( 0.7071067811865486830, 0.7071067811865463515, 0.000000000000000000 ) ) ;
#98524=ORIENTED_EDGE ( 'NONE', *, *, #119693, .T. ) ;
#98525=VERTEX_POINT ( 'NONE', #133645 ) ;
#98526=ORIENTED_EDGE ( 'NONE', *, *, #34673, .F. ) ;
#98527=FACE_OUTER_BOUND ( 'NONE', #30903, .T. ) ;
#98528=DIRECTION ( 'NONE',  ( 0.6830127018922181881, 0.6830127018922202975, -0.2588190451025214056 ) ) ;
#98529=DIRECTION ( 'NONE',  ( 0.000000000000000000, 0.000000000000000000, -1.000000000000000000 ) ) ;
#98530=DIRECTION ( 'NONE',  ( 0.6830127018922181881, 0.6830127018922202975, -0.2588190451025214056 ) ) ;
#98532=CARTESIAN_POINT ( 'NONE',  ( -42.48921356237308800, -27.52281430457085065, 5.000000000000000000 ) ) ;
#98533=EDGE_CURVE ( 'NONE', #6240, #6993, #120586, .T. ) ;
#98534=LINE ( 'NONE', #76821, #31993 ) ;
#98535=DIRECTION ( 'NONE',  ( 0.7071067811865487940, -0.7071067811865463515, 0.000000000000000000 ) ) ;
#98536=CARTESIAN_POINT ( 'NONE',  ( 39.47336096364190183, -5.240707523384228850, 16.25846745537504745 ) ) ;
#98538=DIRECTION ( 'NONE',  ( 0.7071067811865487940, 0.7071067811865463515, 0.000000000000000000 ) ) ;
#98539=EDGE_CURVE ( 'NONE', #65842, #141841, #122020, .T. ) ;
#98540=CARTESIAN_POINT ( 'NONE',  ( -5.483345613589513334, 22.22500000000000142, 4.500000000000000888 ) ) ;
#98541=ORIENTED_EDGE ( 'NONE', *, *, #57503, .F. ) ;
#98542=ORIENTED_EDGE ( 'NONE', *, *, #129713, .T. ) ;
#98543=VERTEX_POINT ( 'NONE', #67707 ) ;
#98544=CARTESIAN_POINT ( 'NONE',  ( -14.29289321881335617, -6.740707523384207533, 5.000000000000000000 ) ) ;
#98545=ORIENTED_EDGE ( 'NONE', *, *, #71108, .F. ) ;
#98546=VERTEX_POINT ( 'NONE', #34322 ) ;
#98547=DIRECTION ( 'NONE',  ( -0.6830127018922180770, -0.6830127018922204085, -0.2588190451025213501 ) ) ;
#98548=DIRECTION ( 'NONE',  ( 0.7071067811865487940, 0.7071067811865463515, 0.000000000000000000 ) ) ;
#98549=EDGE_CURVE ( 'NONE', #42067, #106511, #121320, .T. ) ;
#98550=CARTESIAN_POINT ( 'NONE',  ( 54.29974487139159578, -27.71228299555243879, 4.000000000000000000 ) ) ;
#98551=ORIENTED_EDGE ( 'NONE', *, *, #124615, .T. ) ;
#98553=ORIENTED_EDGE ( 'NONE', *, *, #52142, .F. ) ;
#98554=CARTESIAN_POINT ( 'NONE',  ( -19.49999999999986500, 10.94296225409025247, -9.576120664313302555 ) ) ;
#98555=VECTOR ( 'NONE', #96305, 1000.000000000000000 ) ;
#98557=FACE_OUTER_BOUND ( 'NONE', #79907, .T. ) ;
#98559=ORIENTED_EDGE ( 'NONE', *, *, #21067, .F. ) ;
#98561=DIRECTION ( 'NONE',  ( -0.6830127018922180770, -0.6830127018922204085, -0.2588190451025213501 ) ) ;
#98563=CARTESIAN_POINT ( 'NONE',  ( 13.49999999999991118, -14.94781430457067906, 5.000000000000000000 ) ) ;
#98564=CARTESIAN_POINT ( 'NONE',  ( -5.999999999999956479, -10.44781430457071991, 5.000000000000000000 ) ) ;
#98565=VERTEX_POINT ( 'NONE', #78550 ) ;
#98566=VERTEX_POINT ( 'NONE', #143081 ) ;
#98569=CARTESIAN_POINT ( 'NONE',  ( 34.49999999999975842, -1.535744391599495273, 4.994342998332161443 ) ) ;
#98570=CARTESIAN_POINT ( 'NONE',  ( 6.005480084712508493, 28.92564299267933947, 4.000000000000000000 ) ) ;
#98571=DIRECTION ( 'NONE',  ( 1.000000000000000000, 0.000000000000000000, 0.000000000000000000 ) ) ;
#98572=ORIENTED_EDGE ( 'NONE', *, *, #125645, .F. ) ;
#98573=EDGE_CURVE ( 'NONE', #130643, #15318, #87988, .T. ) ;
#98574=CARTESIAN_POINT ( 'NONE',  ( -12.70679250724066733, 20.25929247661551358, 20.83292124670817813 ) ) ;
#98575=EDGE_CURVE ( 'NONE', #115620, #112794, #127020, .T. ) ;
#98577=CARTESIAN_POINT ( 'NONE',  ( -18.48921356237309510, -27.52281430457068367, 5.000000000000000000 ) ) ;
#98578=ORIENTED_EDGE ( 'NONE', *, *, #50710, .T. ) ;
#98579=LINE ( 'NONE', #12282, #5039 ) ;
#98581=ORIENTED_EDGE ( 'NONE', *, *, #32440, .T. ) ;
#98582=DIRECTION ( 'NONE',  ( -0.7071067811865487940, 0.7071067811865463515, -0.000000000000000000 ) ) ;
#98583=EDGE_LOOP ( 'NONE', ( #116211, #12517, #77716, #115780, #112969 ) ) ;
#98586=CARTESIAN_POINT ( 'NONE',  ( 27.18398860626900060, 28.73617430169806042, 5.000000000000000000 ) ) ;
#98587=CARTESIAN_POINT ( 'NONE',  ( -59.99451991528749772, 28.92564299267980132, 4.000000000000000000 ) ) ;
#98588=VERTEX_POINT ( 'NONE', #114710 ) ;
#98589=LINE ( 'NONE', #96419, #136850 ) ;
#98590=VECTOR ( 'NONE', #68548, 1000.000000000000000 ) ;
#98591=LINE ( 'NONE', #75434, #93823 ) ;
#98594=AXIS2_PLACEMENT_3D ( 'NONE', #37798, #93590, #18118 ) ;
#98595=FACE_OUTER_BOUND ( 'NONE', #15583, .T. ) ;
#98596=CARTESIAN_POINT ( 'NONE',  ( 34.75611968250419181, 16.70565069852387552, 4.955485411084881164 ) ) ;
#98597=VECTOR ( 'NONE', #76185, 1000.000000000000000 ) ;
#98598=CARTESIAN_POINT ( 'NONE',  ( 27.48921356237309155, -27.52281430457074762, 5.000000000000000000 ) ) ;
#98599=DIRECTION ( 'NONE',  ( 0.6830127018922181881, 0.6830127018922202975, -0.2588190451025214056 ) ) ;
#98600=FACE_OUTER_BOUND ( 'NONE', #123999, .T. ) ;
#98601=PLANE ( 'NONE',  #131408 ) ;
#98602=LINE ( 'NONE', #87737, #51471 ) ;
#98606=DIRECTION ( 'NONE',  ( 0.6830127018922180770, -0.6830127018922204085, -0.2588190451025213501 ) ) ;
#98607=ORIENTED_EDGE ( 'NONE', *, *, #122526, .F. ) ;
#98608=VERTEX_POINT ( 'NONE', #137928 ) ;
#98610=VERTEX_POINT ( 'NONE', #46686 ) ;
#98612=ORIENTED_EDGE ( 'NONE', *, *, #137943, .F. ) ;
#98613=LINE ( 'NONE', #142846, #80464 ) ;
#98614=PLANE ( 'NONE',  #9130 ) ;
#98615=VERTEX_POINT ( 'NONE', #27717 ) ;
#98618=CARTESIAN_POINT ( 'NONE',  ( 24.18398860626899705, 28.73617430169804265, 5.000000000000000000 ) ) ;
#98619=LINE ( 'NONE', #142852, #97492 ) ;
#98620=ORIENTED_EDGE ( 'NONE', *, *, #553, .F. ) ;
#98621=EDGE_CURVE ( 'NONE', #60255, #3936, #136477, .T. ) ;
#98623=DIRECTION ( 'NONE',  ( 1.000000000000000000, 0.000000000000000000, 0.000000000000000000 ) ) ;
#98624=CARTESIAN_POINT ( 'NONE',  ( -60.48921356237309510, -27.52281430457097500, 5.000000000000000000 ) ) ;
#98625=DIRECTION ( 'NONE',  ( -0.7071067811865487940, 0.7071067811865463515, 0.000000000000000000 ) ) ;
#98627=PLANE ( 'NONE',  #131112 ) ;
#98630=PLANE ( 'NONE',  #16742 ) ;
#98631=EDGE_CURVE ( 'NONE', #137395, #65995, #60385, .T. ) ;
#98632=EDGE_CURVE ( 'NONE', #119795, #35122, #13255, .T. ) ;
#98633=EDGE_LOOP ( 'NONE', ( #73722, #33515, #96859, #108217 ) ) ;
#98636=EDGE_CURVE ( 'NONE', #75086, #133116, #71251, .T. ) ;
#98638=CARTESIAN_POINT ( 'NONE',  ( 30.29974487139158867, -27.71228299555227537, 4.000000000000000000 ) ) ;
#98639=EDGE_CURVE ( 'NONE', #4786, #97989, #74404, .T. ) ;
#98640=CARTESIAN_POINT ( 'NONE',  ( 0.000000000000000000, 21.72500000000000142, 4.500000000000000888 ) ) ;
#98642=EDGE_CURVE ( 'NONE', #125846, #92174, #5233, .T. ) ;
#98643=LINE ( 'NONE', #45035, #24816 ) ;
#98644=DIRECTION ( 'NONE',  ( 0.3543493200069162685, -0.000000000000000000, -0.9351131265310288487 ) ) ;
#98645=CARTESIAN_POINT ( 'NONE',  ( 2.994519915287485734, 28.92564299267940342, 4.000000000000000000 ) ) ;
#98646=DIRECTION ( 'NONE',  ( -0.7071067811865486830, -0.7071067811865464625, 0.000000000000000000 ) ) ;
#98647=ADVANCED_FACE ( 'NONE', ( #24866 ), #69108, .F. ) ;
#98649=ORIENTED_EDGE ( 'NONE', *, *, #111280, .F. ) ;
#98650=ORIENTED_EDGE ( 'NONE', *, *, #82332, .T. ) ;
#98652=CARTESIAN_POINT ( 'NONE',  ( -33.32816939922329880, -18.74070752338409207, 4.000000000000000000 ) ) ;
#98653=EDGE_CURVE ( 'NONE', #133448, #15838, #48322, .T. ) ;
#98656=VERTEX_POINT ( 'NONE', #26308 ) ;
#98657=CYLINDRICAL_SURFACE ( 'NONE', #86471, 3.378199999999994319 ) ;
#98658=DIRECTION ( 'NONE',  ( 0.7071067811865486830, -0.7071067811865464625, -0.000000000000000000 ) ) ;
#98660=EDGE_CURVE ( 'NONE', #109630, #89139, #29150, .T. ) ;
#98663=ORIENTED_EDGE ( 'NONE', *, *, #137186, .T. ) ;
#98664=AXIS2_PLACEMENT_3D ( 'NONE', #86201, #109367, #32534 ) ;
#98665=DIRECTION ( 'NONE',  ( -0.000000000000000000, -0.3543493200069152693, 0.9351131265310292928 ) ) ;
#98666=VERTEX_POINT ( 'NONE', #8766 ) ;
#98667=EDGE_LOOP ( 'NONE', ( #1105, #72531, #135709, #84077 ) ) ;
#98668=EDGE_LOOP ( 'NONE', ( #66214, #83052, #86341, #123086 ) ) ;
#98669=LINE ( 'NONE', #110242, #111644 ) ;
#98672=VECTOR ( 'NONE', #50019, 1000.000000000000000 ) ;
#98674=DIRECTION ( 'NONE',  ( -0.7071067811865486830, 0.7071067811865464625, 0.000000000000000000 ) ) ;
#98675=EDGE_CURVE ( 'NONE', #4732, #17436, #6631, .T. ) ;
#98677=VECTOR ( 'NONE', #115026, 999.9999999999998863 ) ;
#98678=FACE_BOUND ( 'NONE', #917, .T. ) ;
#98681=FACE_OUTER_BOUND ( 'NONE', #64715, .T. ) ;
#98682=EDGE_LOOP ( 'NONE', ( #41675, #13941, #103685, #93323 ) ) ;
#98683=FACE_OUTER_BOUND ( 'NONE', #35136, .T. ) ;
#98686=CARTESIAN_POINT ( 'NONE',  ( 31.21321903303340406, 12.75929247661558996, 10.29404684609042420 ) ) ;
#98687=ADVANCED_FACE ( 'NONE', ( #52323 ), #95108, .F. ) ;
#98689=VERTEX_POINT ( 'NONE', #63253 ) ;
#98690=AXIS2_PLACEMENT_3D ( 'NONE', #91552, #136461, #93691 ) ;
#98691=AXIS2_PLACEMENT_3D ( 'NONE', #56639, #67495, #111686 ) ;
#98693=ORIENTED_EDGE ( 'NONE', *, *, #128465, .F. ) ;
#98694=DIRECTION ( 'NONE',  ( -0.7071067811865486830, -0.7071067811865464625, 0.000000000000000000 ) ) ;
#98695=ADVANCED_FACE ( 'NONE', ( #17544 ), #61806, .F. ) ;
#98696=CARTESIAN_POINT ( 'NONE',  ( -34.92500000000001137, 21.72500000000000142, 5.000000000000000000 ) ) ;
#98698=CARTESIAN_POINT ( 'NONE',  ( 14.99451991528749595, 28.92564299267948513, 4.000000000000000000 ) ) ;
#98699=LINE ( 'NONE', #119716, #75964 ) ;
#98701=LINE ( 'NONE', #29173, #52505 ) ;
#98702=CARTESIAN_POINT ( 'NONE',  ( 8.816011393731004731, 28.73617430169781173, 5.000000000000000000 ) ) ;
#98705=DIRECTION ( 'NONE',  ( -0.000000000000000000, -0.3543493200069152693, 0.9351131265310292928 ) ) ;
#98708=ORIENTED_EDGE ( 'NONE', *, *, #94489, .T. ) ;
#98709=CARTESIAN_POINT ( 'NONE',  ( 22.49999999999984723, -5.568876922607755908, 4.000000000000000000 ) ) ;
#98710=LINE ( 'NONE', #32041, #74572 ) ;
#98711=ORIENTED_EDGE ( 'NONE', *, *, #129904, .F. ) ;
#98712=EDGE_LOOP ( 'NONE', ( #34430, #127814, #68407, #9784 ) ) ;
#98713=PLANE ( 'NONE',  #103470 ) ;
#98715=CARTESIAN_POINT ( 'NONE',  ( -24.70710678118637560, -12.74070752338414536, 5.000000000000000000 ) ) ;
#98716=EDGE_LOOP ( 'NONE', ( #122971, #138086, #128630, #62465, #124681 ) ) ;
#98717=DIRECTION ( 'NONE',  ( -0.7071067811865486830, 0.7071067811865464625, 0.000000000000000000 ) ) ;
#98718=LINE ( 'NONE', #87148, #109208 ) ;
#98721=VECTOR ( 'NONE', #137624, 1000.000000000000000 ) ;
#98722=CARTESIAN_POINT ( 'NONE',  ( 34.42499999999998295, -12.02281430457047939, 5.000000000000000000 ) ) ;
#98723=ORIENTED_EDGE ( 'NONE', *, *, #82785, .T. ) ;
#98725=CARTESIAN_POINT ( 'NONE',  ( -33.79289321881321939, -2.240707523384264377, 5.000000000000000000 ) ) ;
#98727=DIRECTION ( 'NONE',  ( 1.000000000000000000, 0.000000000000000000, 0.000000000000000000 ) ) ;
#98728=EDGE_LOOP ( 'NONE', ( #36168, #5910, #51644, #62739 ) ) ;
#98729=VECTOR ( 'NONE', #140037, 1000.000000000000000 ) ;
#98730=DIRECTION ( 'NONE',  ( 1.000000000000000000, 0.000000000000000000, 0.000000000000000000 ) ) ;
#98731=VERTEX_POINT ( 'NONE', #16857 ) ;
#98733=PLANE ( 'NONE',  #28517 ) ;
#98734=LINE ( 'NONE', #32808, #58811 ) ;
#98735=ORIENTED_EDGE ( 'NONE', *, *, #135841, .T. ) ;
#98736=ADVANCED_FACE ( 'NONE', ( #97222 ), #51636, .T. ) ;
#98738=DIRECTION ( 'NONE',  ( 0.7071067811865487940, 0.7071067811865463515, 0.000000000000000000 ) ) ;
#98741=ORIENTED_EDGE ( 'NONE', *, *, #76454, .F. ) ;
#98742=LINE ( 'NONE', #132847, #104039 ) ;
#98743=LINE ( 'NONE', #108888, #81722 ) ;
#98744=VERTEX_POINT ( 'NONE', #140749 ) ;
#98745=CARTESIAN_POINT ( 'NONE',  ( -7.499999999999951150, 10.08746187583914633, 4.000000000000000000 ) ) ;
#98746=ORIENTED_EDGE ( 'NONE', *, *, #42775, .F. ) ;
#98747=ADVANCED_FACE ( 'NONE', ( #50207 ), #108103, .F. ) ;
#98748=ORIENTED_EDGE ( 'NONE', *, *, #112981, .F. ) ;
#98749=PLANE ( 'NONE',  #128309 ) ;
#98751=ORIENTED_EDGE ( 'NONE', *, *, #98539, .T. ) ;
#98754=LINE ( 'NONE', #19775, #60007 ) ;
#98755=CARTESIAN_POINT ( 'NONE',  ( -7.019877749285432955, -17.24070752338410273, 20.23474786156467786 ) ) ;
#98757=ORIENTED_EDGE ( 'NONE', *, *, #91218, .T. ) ;
#98758=DIRECTION ( 'NONE',  ( 0.7071067811865487940, -0.7071067811865463515, 0.000000000000000000 ) ) ;
#98759=FACE_OUTER_BOUND ( 'NONE', #26191, .T. ) ;
#98760=CARTESIAN_POINT ( 'NONE',  ( -29.99999999999978328, -15.41253812416060143, 4.000000000000000000 ) ) ;
#98764=EDGE_LOOP ( 'NONE', ( #19019, #11157, #61348, #110834 ) ) ;
#98767=ORIENTED_EDGE ( 'NONE', *, *, #131975, .T. ) ;
#98768=VECTOR ( 'NONE', #91061, 1000.000000000000000 ) ;
#98769=VERTEX_POINT ( 'NONE', #94395 ) ;
#98770=FACE_OUTER_BOUND ( 'NONE', #5589, .T. ) ;
#98771=CARTESIAN_POINT ( 'NONE',  ( -56.99451991528749062, 28.92564299267978001, 4.000000000000000000 ) ) ;
#98772=VERTEX_POINT ( 'NONE', #116161 ) ;
#98774=PLANE ( 'NONE',  #60636 ) ;
#98775=DIRECTION ( 'NONE',  ( 0.7071067811865487940, -0.7071067811865463515, 0.000000000000000000 ) ) ;
#98777=CARTESIAN_POINT ( 'NONE',  ( -3.183988606268992161, 28.73617430169789699, 5.000000000000000000 ) ) ;
#98779=EDGE_LOOP ( 'NONE', ( #131223, #96373, #8070, #24945 ) ) ;
#98780=CARTESIAN_POINT ( 'NONE',  ( -15.29974487139158867, -27.71228299555216879, 4.000000000000000000 ) ) ;
#98783=DIRECTION ( 'NONE',  ( 0.7071067811865487940, 0.7071067811865463515, 0.000000000000000000 ) ) ;
#98784=FACE_OUTER_BOUND ( 'NONE', #32161, .T. ) ;
#98785=VECTOR ( 'NONE', #117539, 1000.000000000000000 ) ;
#98786=CARTESIAN_POINT ( 'NONE',  ( 34.92499999999998295, 22.22500000000000142, 4.000000000000000000 ) ) ;
#98787=CARTESIAN_POINT ( 'NONE',  ( -21.18398860626899349, 28.73617430169802134, 5.000000000000000000 ) ) ;
#98788=AXIS2_PLACEMENT_3D ( 'NONE', #45061, #131308, #31989 ) ;
#98790=LINE ( 'NONE', #99494, #123148 ) ;
#98791=EDGE_CURVE ( 'NONE', #33564, #110484, #129165, .T. ) ;
#98792=CARTESIAN_POINT ( 'NONE',  ( 0.000000000000000000, 0.000000000000000000, 5.000000000000000000 ) ) ;
#98794=EDGE_LOOP ( 'NONE', ( #143350, #3979, #363, #25850 ) ) ;
#98796=EDGE_CURVE ( 'NONE', #126386, #10226, #138643, .T. ) ;
#98797=EDGE_CURVE ( 'NONE', #114851, #32784, #30601, .T. ) ;
#98798=DIRECTION ( 'NONE',  ( -0.7071067811865486830, 0.7071067811865464625, 0.000000000000000000 ) ) ;
#98799=ADVANCED_FACE ( 'NONE', ( #74831 ), #119009, .T. ) ;
#98800=PLANE ( 'NONE',  #76257 ) ;
#98801=EDGE_LOOP ( 'NONE', ( #91817, #126252, #12184, #131050 ) ) ;
#98803=FACE_OUTER_BOUND ( 'NONE', #41437, .T. ) ;
#98804=DIRECTION ( 'NONE',  ( 1.000000000000000000, 0.000000000000000000, 0.000000000000000000 ) ) ;
#98806=VERTEX_POINT ( 'NONE', #45769 ) ;
#98807=ADVANCED_FACE ( 'NONE', ( #42907 ), #142906, .F. ) ;
#98809=ORIENTED_EDGE ( 'NONE', *, *, #1682, .T. ) ;
#98810=EDGE_LOOP ( 'NONE', ( #28103, #16769, #20129, #31320 ) ) ;
#98811=DIRECTION ( 'NONE',  ( -0.7071067811865486830, 0.7071067811865464625, 0.000000000000000000 ) ) ;
#98813=DIRECTION ( 'NONE',  ( -0.000000000000000000, -0.000000000000000000, 1.000000000000000000 ) ) ;
#98814=EDGE_CURVE ( 'NONE', #16402, #126916, #121839, .T. ) ;
#98815=DIRECTION ( 'NONE',  ( -0.7071067811865487940, 0.7071067811865463515, -0.000000000000000000 ) ) ;
#98816=VERTEX_POINT ( 'NONE', #77669 ) ;
#98817=EDGE_CURVE ( 'NONE', #18045, #93380, #53784, .T. ) ;
#98820=VERTEX_POINT ( 'NONE', #67520 ) ;
#98825=VECTOR ( 'NONE', #55068, 1000.000000000000000 ) ;
#98826=DIRECTION ( 'NONE',  ( -0.000000000000000000, -0.3543493200069152693, 0.9351131265310292928 ) ) ;
#98828=EDGE_CURVE ( 'NONE', #34776, #91297, #23242, .T. ) ;
#98829=ORIENTED_EDGE ( 'NONE', *, *, #17686, .T. ) ;
#98830=AXIS2_PLACEMENT_3D ( 'NONE', #139779, #130322, #97666 ) ;
#98832=DIRECTION ( 'NONE',  ( 0.3543493200069162685, -0.000000000000000000, -0.9351131265310288487 ) ) ;
#98836=CARTESIAN_POINT ( 'NONE',  ( 9.812461875839407099, -22.22500000000000142, 4.000000000000000000 ) ) ;
#98837=ORIENTED_EDGE ( 'NONE', *, *, #38789, .T. ) ;
#98839=VECTOR ( 'NONE', #122344, 1000.000000000000000 ) ;
#98840=DIRECTION ( 'NONE',  ( 0.7071067811865487940, 0.7071067811865463515, -0.000000000000000000 ) ) ;
#98841=VERTEX_POINT ( 'NONE', #12380 ) ;
#98842=VERTEX_POINT ( 'NONE', #89936 ) ;
#98843=LINE ( 'NONE', #41617, #11967 ) ;
#98846=CARTESIAN_POINT ( 'NONE',  ( -68.99451991528748351, 28.92564299267986172, 4.000000000000000000 ) ) ;
#98847=EDGE_CURVE ( 'NONE', #142366, #50434, #100828, .T. ) ;
#98848=DIRECTION ( 'NONE',  ( 0.3543493200069162685, -0.000000000000000000, -0.9351131265310288487 ) ) ;
#98849=VECTOR ( 'NONE', #99365, 1000.000000000000000 ) ;
#98850=FACE_BOUND ( 'NONE', #18209, .T. ) ;
#98852=CARTESIAN_POINT ( 'NONE',  ( 51.48921356237309510, -27.52281430457091460, 5.000000000000000000 ) ) ;
#98854=ORIENTED_EDGE ( 'NONE', *, *, #85371, .F. ) ;
#98855=DIRECTION ( 'NONE',  ( -0.7071067811865486830, -0.7071067811865464625, -0.000000000000000000 ) ) ;
#98856=VERTEX_POINT ( 'NONE', #97981 ) ;
#98857=ORIENTED_EDGE ( 'NONE', *, *, #58100, .T. ) ;
#98859=ORIENTED_EDGE ( 'NONE', *, *, #63964, .F. ) ;
#98860=CARTESIAN_POINT ( 'NONE',  ( 21.18398860626899349, 28.73617430169802134, 5.000000000000000000 ) ) ;
#98861=VECTOR ( 'NONE', #82145, 1000.000000000000227 ) ;
#98863=ADVANCED_FACE ( 'NONE', ( #66083 ), #120397, .F. ) ;
#98864=ORIENTED_EDGE ( 'NONE', *, *, #24396, .T. ) ;
#98865=CARTESIAN_POINT ( 'NONE',  ( 27.18398860626900060, 28.73617430169806042, 5.000000000000000000 ) ) ;
#98866=CARTESIAN_POINT ( 'NONE',  ( -34.92500000000001137, -2.781974347153374882, -4.476077389926508943 ) ) ;
#98867=DIRECTION ( 'NONE',  ( -0.000000000000000000, 0.000000000000000000, 1.000000000000000000 ) ) ;
#98868=LINE ( 'NONE', #51832, #138100 ) ;
#98869=EDGE_CURVE ( 'NONE', #114476, #8801, #66783, .T. ) ;
#98870=DIRECTION ( 'NONE',  ( 0.3543493200069162685, -0.000000000000000000, -0.9351131265310288487 ) ) ;
#98871=CARTESIAN_POINT ( 'NONE',  ( -1.499999999999984013, 19.46639925780206326, 5.000000000000000000 ) ) ;
#98872=PLANE ( 'NONE',  #4545 ) ;
#98875=ORIENTED_EDGE ( 'NONE', *, *, #60175, .T. ) ;
#98876=DIRECTION ( 'NONE',  ( 1.000000000000000000, 0.000000000000000000, 0.000000000000000000 ) ) ;
#98877=PLANE ( 'NONE',  #18866 ) ;
#98878=VERTEX_POINT ( 'NONE', #45071 ) ;
#98880=VERTEX_POINT ( 'NONE', #119688 ) ;
#98881=EDGE_CURVE ( 'NONE', #114745, #62013, #11643, .T. ) ;
#98883=VERTEX_POINT ( 'NONE', #134184 ) ;
#98885=VECTOR ( 'NONE', #8006, 1000.000000000000227 ) ;
#98887=DIRECTION ( 'NONE',  ( -0.7071067811865487940, 0.7071067811865463515, -0.000000000000000000 ) ) ;
#98891=ORIENTED_EDGE ( 'NONE', *, *, #96163, .F. ) ;
#98892=DIRECTION ( 'NONE',  ( -0.6830127018922181881, 0.6830127018922202975, -0.2588190451025214056 ) ) ;
#98893=ORIENTED_EDGE ( 'NONE', *, *, #105617, .F. ) ;
#98895=VECTOR ( 'NONE', #120018, 999.9999999999998863 ) ;
#98896=CARTESIAN_POINT ( 'NONE',  ( 10.17183060077639745, 18.75929247661552779, 4.000000000000000000 ) ) ;
#98897=CARTESIAN_POINT ( 'NONE',  ( 60.48921356237309510, -27.52281430457097500, 5.000000000000000000 ) ) ;
#98898=VERTEX_POINT ( 'NONE', #78374 ) ;
#98899=ORIENTED_EDGE ( 'NONE', *, *, #70383, .T. ) ;
#98900=LINE ( 'NONE', #7040, #79726 ) ;
#98901=PLANE ( 'NONE',  #5187 ) ;
#98902=LINE ( 'NONE', #132300, #97978 ) ;
#98903=VERTEX_POINT ( 'NONE', #32001 ) ;
#98904=DIRECTION ( 'NONE',  ( 0.7071067811865487940, 0.7071067811865463515, 0.000000000000000000 ) ) ;
#98905=ADVANCED_FACE ( 'NONE', ( #55922 ), #54496, .F. ) ;
#98906=ORIENTED_EDGE ( 'NONE', *, *, #102805, .T. ) ;
#98907=EDGE_LOOP ( 'NONE', ( #65936, #77186, #137745, #100260 ) ) ;
#98909=DIRECTION ( 'NONE',  ( -0.7071067811865486830, -0.7071067811865464625, -0.000000000000000000 ) ) ;
#98911=CARTESIAN_POINT ( 'NONE',  ( 4.499999999999968914, -6.839392718269127869, -8.480912228396096708 ) ) ;
#98912=FACE_OUTER_BOUND ( 'NONE', #39929, .T. ) ;
#98913=CARTESIAN_POINT ( 'NONE',  ( 60.18398860626900415, 28.73617430169829490, 5.000000000000000000 ) ) ;
#98914=ADVANCED_FACE ( 'NONE', ( #44338 ), #87103, .F. ) ;
#98915=PLANE ( 'NONE',  #59955 ) ;
#98916=EDGE_LOOP ( 'NONE', ( #90995, #114645, #17749, #124379 ) ) ;
#98918=CARTESIAN_POINT ( 'NONE',  ( 11.29289321881337393, 8.259292476615636147, 5.000000000000000000 ) ) ;
#98919=VERTEX_POINT ( 'NONE', #65384 ) ;
#98920=VECTOR ( 'NONE', #75888, 1000.000000000000000 ) ;
#98921=DIRECTION ( 'NONE',  ( 0.7071067811865486830, -0.7071067811865464625, -0.000000000000000000 ) ) ;
#98922=DIRECTION ( 'NONE',  ( 0.7071067811865487940, 0.7071067811865463515, -0.000000000000000000 ) ) ;
#98924=VERTEX_POINT ( 'NONE', #109560 ) ;
#98925=CARTESIAN_POINT ( 'NONE',  ( 10.00193056682090642, -22.22500000000000142, 4.500000000000000888 ) ) ;
#98926=CARTESIAN_POINT ( 'NONE',  ( -60.18398860626900415, 28.73617430169829490, 5.000000000000000000 ) ) ;
#98928=VERTEX_POINT ( 'NONE', #33469 ) ;
#98929=ORIENTED_EDGE ( 'NONE', *, *, #26029, .F. ) ;
#98930=CARTESIAN_POINT ( 'NONE',  ( 4.499999999999979572, 7.087461875839172087, 4.000000000000000000 ) ) ;
#98932=DIRECTION ( 'NONE',  ( -0.7071067811865487940, 0.7071067811865463515, 0.000000000000000000 ) ) ;
#98933=VECTOR ( 'NONE', #13407, 1000.000000000000000 ) ;
#98934=CARTESIAN_POINT ( 'NONE',  ( -26.70025512860841488, -27.71228299555187391, 4.000000000000000000 ) ) ;
#98937=ADVANCED_FACE ( 'NONE', ( #10237 ), #37, .F. ) ;
#98938=DIRECTION ( 'NONE',  ( 0.7071067811865487940, 0.7071067811865463515, 0.000000000000000000 ) ) ;
#98939=CARTESIAN_POINT ( 'NONE',  ( -54.29974487139159578, -27.71228299555243879, 4.000000000000000000 ) ) ;
#98941=LINE ( 'NONE', #116064, #95020 ) ;
#98942=ORIENTED_EDGE ( 'NONE', *, *, #118218, .T. ) ;
#98943=CARTESIAN_POINT ( 'NONE',  ( 11.99999999999992184, -6.412538124160689357, 4.000000000000000000 ) ) ;
#98945=VERTEX_POINT ( 'NONE', #136304 ) ;
#98946=DIRECTION ( 'NONE',  ( -0.7071067811865486830, -0.7071067811865464625, 0.000000000000000000 ) ) ;
#98947=CARTESIAN_POINT ( 'NONE',  ( -27.18398860626900060, 28.73617430169806042, 5.000000000000000000 ) ) ;
#98948=DIRECTION ( 'NONE',  ( -0.000000000000000000, 0.3543493200069153248, 0.9351131265310292928 ) ) ;
#98949=CARTESIAN_POINT ( 'NONE',  ( -13.49999999999990052, 0.4311230773921797543, 4.000000000000000000 ) ) ;
#98951=CARTESIAN_POINT ( 'NONE',  ( -20.18753812416038329, -22.22500000000000142, 4.000000000000000000 ) ) ;
#98952=CARTESIAN_POINT ( 'NONE',  ( -23.93988928955965889, -9.740707523384180888, 10.89222023123386585 ) ) ;
#98953=ORIENTED_EDGE ( 'NONE', *, *, #54102, .F. ) ;
#98956=DIRECTION ( 'NONE',  ( 0.7071067811865487940, 0.7071067811865463515, 0.000000000000000000 ) ) ;
#98957=CARTESIAN_POINT ( 'NONE',  ( -0.2997448713915885632, -27.71228299555206220, 4.000000000000000000 ) ) ;
#98959=LINE ( 'NONE', #133758, #27799 ) ;
#98960=ADVANCED_FACE ( 'NONE', ( #2934 ), #37736, .F. ) ;
#98961=CARTESIAN_POINT ( 'NONE',  ( -6.183988606268994381, 28.73617430169791476, 5.000000000000000000 ) ) ;
#98962=ORIENTED_EDGE ( 'NONE', *, *, #43420, .T. ) ;
#98965=DIRECTION ( 'NONE',  ( -0.7071067811865486830, -0.7071067811865464625, -0.000000000000000000 ) ) ;
#98967=CARTESIAN_POINT ( 'NONE',  ( -24.32816939922335919, -0.7407075233842701500, 4.000000000000000000 ) ) ;
#98968=FACE_OUTER_BOUND ( 'NONE', #27676, .T. ) ;
#98969=EDGE_LOOP ( 'NONE', ( #70035, #47715, #142539, #131110 ) ) ;
#98970=ADVANCED_FACE ( 'NONE', ( #79842 ), #13786, .F. ) ;
#98971=ADVANCED_FACE ( 'NONE', ( #3615 ), #124019, .F. ) ;
#98972=DIRECTION ( 'NONE',  ( 0.7071067811865486830, -0.7071067811865464625, -0.000000000000000000 ) ) ;
#98973=ORIENTED_EDGE ( 'NONE', *, *, #113138, .F. ) ;
#98975=DIRECTION ( 'NONE',  ( 0.7071067811865486830, -0.7071067811865464625, -0.000000000000000000 ) ) ;
#98977=LINE ( 'NONE', #103107, #47771 ) ;
#98978=ORIENTED_EDGE ( 'NONE', *, *, #76222, .T. ) ;
#98980=VECTOR ( 'NONE', #81098, 1000.000000000000000 ) ;
#98981=DIRECTION ( 'NONE',  ( 1.000000000000000000, 0.000000000000000000, 0.000000000000000000 ) ) ;
#98982=CARTESIAN_POINT ( 'NONE',  ( -84.29974487139159578, -27.71228299555264840, 4.000000000000000000 ) ) ;
#98984=EDGE_CURVE ( 'NONE', #112859, #81705, #115225, .T. ) ;
#98986=ADVANCED_FACE ( 'NONE', ( #15214 ), #102282, .F. ) ;
#98987=FACE_OUTER_BOUND ( 'NONE', #128800, .T. ) ;
#98988=LINE ( 'NONE', #119310, #35983 ) ;
#98989=VERTEX_POINT ( 'NONE', #123326 ) ;
#98991=PLANE ( 'NONE',  #38385 ) ;
#98992=CARTESIAN_POINT ( 'NONE',  ( 16.49999999999988987, -13.53360074219760278, 5.000000000000000000 ) ) ;
#98993=VECTOR ( 'NONE', #60956, 1000.000000000000000 ) ;
#98994=VECTOR ( 'NONE', #55204, 1000.000000000000000 ) ;
#98995=ORIENTED_EDGE ( 'NONE', *, *, #78535, .F. ) ;
#98996=ADVANCED_FACE ( 'NONE', ( #49342 ), #47909, .F. ) ;
#98997=EDGE_LOOP ( 'NONE', ( #32418, #90412, #57910, #91063 ) ) ;
#99000=CARTESIAN_POINT ( 'NONE',  ( 5.510786437626906675, -27.52281430457051314, 5.000000000000000000 ) ) ;
#99005=VERTEX_POINT ( 'NONE', #48593 ) ;
#99006=EDGE_CURVE ( 'NONE', #9403, #139296, #26132, .T. ) ;
#99007=CARTESIAN_POINT ( 'NONE',  ( 16.49999999999988276, -5.568876922607752356, 4.000000000000000000 ) ) ;
#99009=ORIENTED_EDGE ( 'NONE', *, *, #29855, .T. ) ;
#99010=DIRECTION ( 'NONE',  ( 0.7071067811865487940, -0.7071067811865463515, 0.000000000000000000 ) ) ;
#99011=CARTESIAN_POINT ( 'NONE',  ( -4.499999999999966249, 9.431123077392085108, 4.000000000000000000 ) ) ;
#99012=EDGE_CURVE ( 'NONE', #85868, #78770, #70396, .T. ) ;
#99013=CARTESIAN_POINT ( 'NONE',  ( -33.70701326429281153, -21.74070752338405299, 4.999753212805220670 ) ) ;
#99015=CARTESIAN_POINT ( 'NONE',  ( 10.82816939922345689, 0.7592924766157113092, 4.000000000000000000 ) ) ;
#99016=PLANE ( 'NONE',  #61856 ) ;
#99017=ADVANCED_FACE ( 'NONE', ( #30411 ), #139907, .F. ) ;
#99018=CARTESIAN_POINT ( 'NONE',  ( -8.994519915287490619, 28.92564299267944250, 4.000000000000000000 ) ) ;
#99019=CARTESIAN_POINT ( 'NONE',  ( 0.000000000000000000, 0.000000000000000000, 5.000000000000000000 ) ) ;
#99020=VECTOR ( 'NONE', #112449, 1000.000000000000000 ) ;
#99022=DIRECTION ( 'NONE',  ( -0.000000000000000000, 0.000000000000000000, 1.000000000000000000 ) ) ;
#99023=DIRECTION ( 'NONE',  ( 0.7071067811865487940, 0.7071067811865463515, 0.000000000000000000 ) ) ;
#99024=EDGE_CURVE ( 'NONE', #141704, #4133, #139196, .T. ) ;
#99025=VERTEX_POINT ( 'NONE', #50032 ) ;
#99026=EDGE_LOOP ( 'NONE', ( #65629, #25683, #18140, #122995 ) ) ;
#99030=LINE ( 'NONE', #25042, #95611 ) ;
#99031=CARTESIAN_POINT ( 'NONE',  ( -31.49999999999979039, -1.592773361805400301, -6.492772025301160710 ) ) ;
#99032=CARTESIAN_POINT ( 'NONE',  ( 6.489213562373093325, -27.52281430457059841, 5.000000000000000000 ) ) ;
#99033=ORIENTED_EDGE ( 'NONE', *, *, #13389, .T. ) ;
#99035=PLANE ( 'NONE',  #70359 ) ;
#99036=FACE_BOUND ( 'NONE', #57084, .T. ) ;
#99037=CARTESIAN_POINT ( 'NONE',  ( 0.000000000000000000, 0.000000000000000000, 5.000000000000000000 ) ) ;
#99038=LINE ( 'NONE', #1149, #64637 ) ;
#99040=VERTEX_POINT ( 'NONE', #116698 ) ;
#99041=DIRECTION ( 'NONE',  ( -0.000000000000000000, 0.000000000000000000, 1.000000000000000000 ) ) ;
#99042=FACE_OUTER_BOUND ( 'NONE', #129258, .T. ) ;
#99043=ORIENTED_EDGE ( 'NONE', *, *, #141979, .T. ) ;
#99044=ORIENTED_EDGE ( 'NONE', *, *, #127401, .F. ) ;
#99047=EDGE_LOOP ( 'NONE', ( #115384, #55902, #63045, #132625 ) ) ;
#99048=FACE_OUTER_BOUND ( 'NONE', #86006, .T. ) ;
#99050=VECTOR ( 'NONE', #78043, 1000.000000000000227 ) ;
#99052=DIRECTION ( 'NONE',  ( 0.7071067811865487940, 0.7071067811865463515, 0.000000000000000000 ) ) ;
#99053=CARTESIAN_POINT ( 'NONE',  ( 4.966599676569746435, 6.759292476615653023, 12.28218704918523230 ) ) ;
#99055=FACE_OUTER_BOUND ( 'NONE', #94152, .T. ) ;
#99056=PLANE ( 'NONE',  #102641 ) ;
#99057=DIRECTION ( 'NONE',  ( 1.000000000000000000, 0.000000000000000000, 0.000000000000000000 ) ) ;
#99058=DIRECTION ( 'NONE',  ( 1.000000000000000000, 0.000000000000000000, 0.000000000000000000 ) ) ;
#99059=EDGE_LOOP ( 'NONE', ( #107186, #16719, #45947, #106281 ) ) ;
#99061=ORIENTED_EDGE ( 'NONE', *, *, #6508, .F. ) ;
#99062=ORIENTED_EDGE ( 'NONE', *, *, #101746, .T. ) ;
#99063=VERTEX_POINT ( 'NONE', #29671 ) ;
#99065=ORIENTED_EDGE ( 'NONE', *, *, #67109, .T. ) ;
#99066=VECTOR ( 'NONE', #112127, 1000.000000000000227 ) ;
#99067=CARTESIAN_POINT ( 'NONE',  ( 45.29974487139158867, -27.71228299555237840, 4.000000000000000000 ) ) ;
#99068=AXIS2_PLACEMENT_3D ( 'NONE', #58278, #24169, #57533 ) ;
#99069=EDGE_CURVE ( 'NONE', #25861, #6819, #82656, .T. ) ;
#99071=EDGE_LOOP ( 'NONE', ( #62437, #48606, #123705, #79204 ) ) ;
#99072=EDGE_CURVE ( 'NONE', #100985, #474, #18054, .T. ) ;
#99073=CARTESIAN_POINT ( 'NONE',  ( 20.47599861414536448, 22.03583458319438648, 4.979811245910087614 ) ) ;
#99074=VERTEX_POINT ( 'NONE', #63768 ) ;
#99075=VECTOR ( 'NONE', #131347, 999.9999999999998863 ) ;
#99076=VECTOR ( 'NONE', #137768, 1000.000000000000000 ) ;
#99078=DIRECTION ( 'NONE',  ( -0.000000000000000000, 0.3543493200069153248, 0.9351131265310292928 ) ) ;
#99079=CARTESIAN_POINT ( 'NONE',  ( 54.18398860626899705, 28.73617430169825226, 5.000000000000000000 ) ) ;
#99080=EDGE_CURVE ( 'NONE', #49447, #141655, #39149, .T. ) ;
#99081=CARTESIAN_POINT ( 'NONE',  ( -20.20710678118639692, -5.240707523384227073, 5.000000000000000000 ) ) ;
#99082=ORIENTED_EDGE ( 'NONE', *, *, #30022, .T. ) ;
#99083=ORIENTED_EDGE ( 'NONE', *, *, #102124, .F. ) ;
#99084=EDGE_LOOP ( 'NONE', ( #137838, #38559, #100493, #66085 ) ) ;
#99086=LINE ( 'NONE', #494, #118208 ) ;
#99087=CARTESIAN_POINT ( 'NONE',  ( -30.18398860626900060, 28.73617430169808173, 5.000000000000000000 ) ) ;
#99088=DIRECTION ( 'NONE',  ( -0.6830127018922180770, -0.6830127018922204085, -0.2588190451025213501 ) ) ;
#99090=CARTESIAN_POINT ( 'NONE',  ( 19.49999999999985434, -17.94781430457064531, 5.000000000000000000 ) ) ;
#99091=CARTESIAN_POINT ( 'NONE',  ( -11.99999999999991651, 4.931123077392129517, 4.000000000000000000 ) ) ;
#99092=DIRECTION ( 'NONE',  ( 0.7071067811865487940, 0.7071067811865463515, 0.000000000000000000 ) ) ;
#99093=CARTESIAN_POINT ( 'NONE',  ( -23.14994871458961967, -8.240707523384193323, 17.25253755692233781 ) ) ;
#99094=ORIENTED_EDGE ( 'NONE', *, *, #3701, .T. ) ;
#99095=DIRECTION ( 'NONE',  ( -0.7071067811865486830, -0.7071067811865464625, -0.000000000000000000 ) ) ;
#99096=ORIENTED_EDGE ( 'NONE', *, *, #37001, .F. ) ;
#99097=EDGE_CURVE ( 'NONE', #80191, #124824, #118835, .T. ) ;
#99098=FACE_OUTER_BOUND ( 'NONE', #4086, .T. ) ;
#99099=EDGE_LOOP ( 'NONE', ( #9151, #110677, #31805, #108803 ) ) ;
#99101=VECTOR ( 'NONE', #4555, 1000.000000000000227 ) ;
#99102=CARTESIAN_POINT ( 'NONE',  ( 36.18398860626899705, 28.73617430169812437, 5.000000000000000000 ) ) ;
#99104=VERTEX_POINT ( 'NONE', #117381 ) ;
#99105=DIRECTION ( 'NONE',  ( -0.7071067811865487940, 0.7071067811865463515, -0.000000000000000000 ) ) ;
#99106=ORIENTED_EDGE ( 'NONE', *, *, #135630, .F. ) ;
#99107=DIRECTION ( 'NONE',  ( -0.7071067811865486830, -0.7071067811865463515, 0.000000000000000000 ) ) ;
#99108=VECTOR ( 'NONE', #11490, 1000.000000000000000 ) ;
#99109=ORIENTED_EDGE ( 'NONE', *, *, #91764, .T. ) ;
#99110=CARTESIAN_POINT ( 'NONE',  ( -2.999999999999975131, 17.96639925780208102, 5.000000000000000000 ) ) ;
#99112=CARTESIAN_POINT ( 'NONE',  ( -31.49999999999977973, 4.466399257802215139, 5.000000000000000000 ) ) ;
#99115=LINE ( 'NONE', #108551, #94556 ) ;
#99116=CARTESIAN_POINT ( 'NONE',  ( -34.92500000000001137, 22.22500000000000142, 4.000000000000000000 ) ) ;
#99117=EDGE_CURVE ( 'NONE', #97669, #68590, #105790, .T. ) ;
#99118=DIRECTION ( 'NONE',  ( -0.000000000000000000, 0.3543493200069153248, 0.9351131265310292928 ) ) ;
#99121=VECTOR ( 'NONE', #104214, 1000.000000000000000 ) ;
#99122=LINE ( 'NONE', #1242, #4898 ) ;
#99123=PLANE ( 'NONE',  #96402 ) ;
#99124=ORIENTED_EDGE ( 'NONE', *, *, #104730, .T. ) ;
#99125=VECTOR ( 'NONE', #102702, 1000.000000000000227 ) ;
#99127=VERTEX_POINT ( 'NONE', #16664 ) ;
#99128=ADVANCED_FACE ( 'NONE', ( #40585 ), #107928, .F. ) ;
#99129=DIRECTION ( 'NONE',  ( 0.7071067811865486830, -0.7071067811865464625, -0.000000000000000000 ) ) ;
#99130=VERTEX_POINT ( 'NONE', #137759 ) ;
#99131=CARTESIAN_POINT ( 'NONE',  ( -0.9891197134605101970, -22.02621442084248216, 4.990779571109223767 ) ) ;
#99132=DIRECTION ( 'NONE',  ( -0.7071067811865487940, 0.7071067811865463515, 0.000000000000000000 ) ) ;
#99133=CARTESIAN_POINT ( 'NONE',  ( -9.489213562373095101, -27.52281430457062328, 5.000000000000000000 ) ) ;
#99135=ORIENTED_EDGE ( 'NONE', *, *, #140665, .T. ) ;
#99137=FACE_OUTER_BOUND ( 'NONE', #68022, .T. ) ;
#99138=CARTESIAN_POINT ( 'NONE',  ( -29.99999999999977973, -13.44781430457069149, 5.000000000000000000 ) ) ;
#99139=CARTESIAN_POINT ( 'NONE',  ( 3.792893218813434775, -2.240707523384260824, 5.000000000000000000 ) ) ;
#99141=CARTESIAN_POINT ( 'NONE',  ( 34.92499999999998295, 10.51246187583937441, 4.000000000000000000 ) ) ;
#99142=EDGE_CURVE ( 'NONE', #80484, #71410, #77511, .T. ) ;
#99143=CARTESIAN_POINT ( 'NONE',  ( 5.816011393731002066, 28.73617430169783304, 5.000000000000000000 ) ) ;
#99144=LINE ( 'NONE', #122328, #91442 ) ;
#99146=CARTESIAN_POINT ( 'NONE',  ( -2.700255128608413990, -27.71228299555204089, 4.000000000000000000 ) ) ;
#99148=DIRECTION ( 'NONE',  ( 0.7071067811865487940, 0.7071067811865463515, -0.000000000000000000 ) ) ;
#99149=CARTESIAN_POINT ( 'NONE',  ( 32.99999999999976552, -3.033600742197707145, 5.000000000000000000 ) ) ;
#99150=EDGE_LOOP ( 'NONE', ( #110074, #63816, #19789, #54617, #57477 ) ) ;
#99151=ORIENTED_EDGE ( 'NONE', *, *, #141852, .F. ) ;
#99152=VERTEX_POINT ( 'NONE', #21676 ) ;
#99154=AXIS2_PLACEMENT_3D ( 'NONE', #109761, #54688, #85147 ) ;
#99155=ORIENTED_EDGE ( 'NONE', *, *, #60664, .F. ) ;
#99157=LINE ( 'NONE', #56456, #50328 ) ;
#99158=DIRECTION ( 'NONE',  ( 0.7071067811865487940, -0.7071067811865463515, 0.000000000000000000 ) ) ;
#99159=ORIENTED_EDGE ( 'NONE', *, *, #49080, .F. ) ;
#99160=EDGE_CURVE ( 'NONE', #141003, #7076, #86229, .T. ) ;
#99161=CARTESIAN_POINT ( 'NONE',  ( -31.49999999999977973, 15.43112307739202471, 4.000000000000000000 ) ) ;
#99164=VERTEX_POINT ( 'NONE', #89090 ) ;
#99165=CARTESIAN_POINT ( 'NONE',  ( 42.48921356237308800, -27.52281430457085065, 5.000000000000000000 ) ) ;
#99167=VECTOR ( 'NONE', #117261, 1000.000000000000000 ) ;
#99168=VERTEX_POINT ( 'NONE', #12208 ) ;
#99169=ORIENTED_EDGE ( 'NONE', *, *, #34243, .F. ) ;
#99170=VECTOR ( 'NONE', #134181, 1000.000000000000227 ) ;
#99171=ORIENTED_EDGE ( 'NONE', *, *, #28880, .F. ) ;
#99173=AXIS2_PLACEMENT_3D ( 'NONE', #72420, #62953, #96231 ) ;
#99174=CARTESIAN_POINT ( 'NONE',  ( 14.99999999999990230, 14.58746187583908416, 4.000000000000000000 ) ) ;
#99176=CARTESIAN_POINT ( 'NONE',  ( -24.48921356237309510, -27.52281430457072631, 5.000000000000000000 ) ) ;
#99177=VECTOR ( 'NONE', #10099, 1000.000000000000227 ) ;
#99178=VECTOR ( 'NONE', #40431, 1000.000000000000000 ) ;
#99180=CARTESIAN_POINT ( 'NONE',  ( 3.328169399223498637, 11.25929247661560417, 4.000000000000000000 ) ) ;
#99181=EDGE_CURVE ( 'NONE', #34556, #20392, #65925, .T. ) ;
#99183=EDGE_CURVE ( 'NONE', #28440, #60272, #141301, .T. ) ;
#99184=EDGE_LOOP ( 'NONE', ( #35292, #24856, #12460, #132717 ) ) ;
#99185=EDGE_LOOP ( 'NONE', ( #64859, #61820, #134890, #43119 ) ) ;
#99186=CARTESIAN_POINT ( 'NONE',  ( 25.49999999999982592, 14.14708470758593251, -0.5283514160167148699 ) ) ;
#99187=VERTEX_POINT ( 'NONE', #33309 ) ;
#99188=ORIENTED_EDGE ( 'NONE', *, *, #135517, .T. ) ;
#99189=VECTOR ( 'NONE', #40146, 1000.000000000000000 ) ;
#99190=EDGE_CURVE ( 'NONE', #56507, #1974, #119518, .T. ) ;
#99192=CARTESIAN_POINT ( 'NONE',  ( 14.99999999999989519, 7.559798855135672291, 4.979909187984731922 ) ) ;
#99193=EDGE_LOOP ( 'NONE', ( #134584, #103945, #61049, #39767 ) ) ;
#99194=LINE ( 'NONE', #53596, #138642 ) ;
#99196=FACE_OUTER_BOUND ( 'NONE', #16887, .T. ) ;
#99199=VERTEX_POINT ( 'NONE', #22349 ) ;
#99200=VECTOR ( 'NONE', #109998, 1000.000000000000000 ) ;
#99201=DIRECTION ( 'NONE',  ( 0.000000000000000000, -1.000000000000000000, 0.000000000000000000 ) ) ;
#99202=VECTOR ( 'NONE', #115247, 1000.000000000000000 ) ;
#99203=EDGE_LOOP ( 'NONE', ( #92039, #71238, #60081, #107647, #27980, #25795 ) ) ;
#99204=CARTESIAN_POINT ( 'NONE',  ( -7.499999999999940492, -2.947814304570798960, 5.000000000000000000 ) ) ;
#99207=ORIENTED_EDGE ( 'NONE', *, *, #59788, .F. ) ;
#99208=LINE ( 'NONE', #142059, #48204 ) ;
#99209=VERTEX_POINT ( 'NONE', #75354 ) ;
#99210=ORIENTED_EDGE ( 'NONE', *, *, #117429, .T. ) ;
#99212=ORIENTED_EDGE ( 'NONE', *, *, #129977, .T. ) ;
#99213=VECTOR ( 'NONE', #45617, 1000.000000000000227 ) ;
#99214=LINE ( 'NONE', #110103, #102136 ) ;
#99215=DIRECTION ( 'NONE',  ( 0.6830127018922180770, -0.6830127018922204085, -0.2588190451025213501 ) ) ;
#99216=DIRECTION ( 'NONE',  ( -0.7071067811865486830, 0.7071067811865464625, 0.000000000000000000 ) ) ;
#99218=DIRECTION ( 'NONE',  ( 0.6830127018922180770, -0.6830127018922204085, -0.2588190451025213501 ) ) ;
#99219=ADVANCED_FACE ( 'NONE', ( #20215 ), #110788, .T. ) ;
#99220=FACE_OUTER_BOUND ( 'NONE', #30572, .T. ) ;
#99224=LINE ( 'NONE', #45623, #104901 ) ;
#99225=CARTESIAN_POINT ( 'NONE',  ( 54.48921356237310221, -27.52281430457093236, 5.000000000000000000 ) ) ;
#99226=CARTESIAN_POINT ( 'NONE',  ( 32.99999999999977973, 11.96639925780213787, 5.000000000000000000 ) ) ;
#99227=DIRECTION ( 'NONE',  ( 0.7071067811865487940, 0.7071067811865463515, 0.000000000000000000 ) ) ;
#99228=EDGE_LOOP ( 'NONE', ( #109917, #39842, #64983, #113605 ) ) ;
#99229=ORIENTED_EDGE ( 'NONE', *, *, #11265, .F. ) ;
#99230=ORIENTED_EDGE ( 'NONE', *, *, #116855, .F. ) ;
#99231=CARTESIAN_POINT ( 'NONE',  ( -36.48921356237310221, -27.52281430457080802, 5.000000000000000000 ) ) ;
#99232=VERTEX_POINT ( 'NONE', #120972 ) ;
#99233=EDGE_CURVE ( 'NONE', #3063, #121049, #10068, .T. ) ;
#99238=DIRECTION ( 'NONE',  ( 0.7071067811865486830, -0.7071067811865464625, -0.000000000000000000 ) ) ;
#99239=LINE ( 'NONE', #20984, #99580 ) ;
#99240=ORIENTED_EDGE ( 'NONE', *, *, #99636, .F. ) ;
#99241=CARTESIAN_POINT ( 'NONE',  ( 36.18398860626899705, 28.73617430169812437, 5.000000000000000000 ) ) ;
#99243=DIRECTION ( 'NONE',  ( -0.7071067811865486830, 0.7071067811865464625, 0.000000000000000000 ) ) ;
#99245=EDGE_CURVE ( 'NONE', #141085, #58174, #613, .T. ) ;
#99247=EDGE_LOOP ( 'NONE', ( #79839, #104298, #97251, #74927 ) ) ;
#99249=CARTESIAN_POINT ( 'NONE',  ( -14.70025512860841133, -27.71228299555195917, 4.000000000000000000 ) ) ;
#99250=ADVANCED_FACE ( 'NONE', ( #68083 ), #135452, .F. ) ;
#99251=DIRECTION ( 'NONE',  ( -0.7071067811865487940, 0.7071067811865463515, 0.000000000000000000 ) ) ;
#99254=ORIENTED_EDGE ( 'NONE', *, *, #129635, .F. ) ;
#99255=CARTESIAN_POINT ( 'NONE',  ( -28.82816939922332722, 6.759292476615653023, 4.000000000000000000 ) ) ;
#99256=LINE ( 'NONE', #111592, #127338 ) ;
#99257=CARTESIAN_POINT ( 'NONE',  ( -5.994519915287488843, 28.92564299267942118, 4.000000000000000000 ) ) ;
#99258=CARTESIAN_POINT ( 'NONE',  ( -15.77004279457781877, 21.73644205237996729, 5.000000000000000888 ) ) ;
#99259=DIRECTION ( 'NONE',  ( -0.7071067811865486830, -0.7071067811865464625, 0.000000000000000000 ) ) ;
#99261=LINE ( 'NONE', #40648, #18328 ) ;
#99262=EDGE_CURVE ( 'NONE', #467, #54775, #136852, .T. ) ;
#99263=VECTOR ( 'NONE', #8665, 1000.000000000000000 ) ;
#99265=DIRECTION ( 'NONE',  ( 0.7071067811865487940, -0.7071067811865463515, 0.000000000000000000 ) ) ;
#99267=EDGE_CURVE ( 'NONE', #12409, #50067, #114385, .T. ) ;
#99268=CARTESIAN_POINT ( 'NONE',  ( -34.60428828362105236, 22.19175015946030882, 4.000000000000000000 ) ) ;
#99269=AXIS2_PLACEMENT_3D ( 'NONE', #132978, #132263, #114563 ) ;
#99270=ADVANCED_FACE ( 'NONE', ( #103487 ), #2764, .T. ) ;
#99271=VECTOR ( 'NONE', #70102, 999.9999999999998863 ) ;
#99272=AXIS2_PLACEMENT_3D ( 'NONE', #113836, #14533, #58812 ) ;
#99273=CARTESIAN_POINT ( 'NONE',  ( 6.489213562373093325, -27.52281430457059841, 5.000000000000000000 ) ) ;
#99274=ORIENTED_EDGE ( 'NONE', *, *, #38769, .T. ) ;
#99275=VECTOR ( 'NONE', #6453, 1000.000000000000000 ) ;
#99276=DIRECTION ( 'NONE',  ( 0.3543493200069162685, -0.000000000000000000, -0.9351131265310288487 ) ) ;
#99277=ORIENTED_EDGE ( 'NONE', *, *, #24860, .T. ) ;
#99279=CARTESIAN_POINT ( 'NONE',  ( 8.673617379884035472E-15, 2.587461875839212944, 4.000000000000000000 ) ) ;
#99280=CARTESIAN_POINT ( 'NONE',  ( 69.18398860626899705, 28.73617430169835529, 5.000000000000000000 ) ) ;
#99281=ADVANCED_FACE ( 'NONE', ( #125271 ), #59334, .F. ) ;
#99282=ORIENTED_EDGE ( 'NONE', *, *, #59991, .F. ) ;
#99283=LINE ( 'NONE', #85564, #62791 ) ;
#99285=( BOUNDED_CURVE ( )  B_SPLINE_CURVE ( 3, ( #27692, #103803, #4449, #48756 ),
 .UNSPECIFIED., .F., .T. ) 
 B_SPLINE_CURVE_WITH_KNOTS ( ( 4, 4 ),
 ( 3.858351980207623821, 3.926990816987242727 ),
 .UNSPECIFIED. ) 
 CURVE ( )  GEOMETRIC_REPRESENTATION_ITEM ( )  RATIONAL_B_SPLINE_CURVE ( ( 1.000000000000000000, 0.9996074310407763175, 0.9996074310407763175, 1.000000000000000000 ) ) 
 REPRESENTATION_ITEM ( '' )  );
#99286=FACE_OUTER_BOUND ( 'NONE', #47289, .T. ) ;
#99289=DIRECTION ( 'NONE',  ( -0.3543493200069162685, -0.000000000000000000, -0.9351131265310288487 ) ) ;
#99290=LINE ( 'NONE', #47149, #67725 ) ;
#99291=DIRECTION ( 'NONE',  ( -0.3543493200069162685, -0.000000000000000000, -0.9351131265310288487 ) ) ;
#99292=ADVANCED_FACE ( 'NONE', ( #91916 ), #57906, .F. ) ;
#99294=PLANE ( 'NONE',  #50284 ) ;
#99295=LINE ( 'NONE', #63862, #32969 ) ;
#99296=AXIS2_PLACEMENT_3D ( 'NONE', #101442, #123230, #34073 ) ;
#99298=CARTESIAN_POINT ( 'NONE',  ( 13.49999999999991118, 10.08746187583914278, 4.000000000000000000 ) ) ;
#99299=CARTESIAN_POINT ( 'NONE',  ( -23.57322811595262735, -0.7198850472490149199, 4.205258209906618028 ) ) ;
#99300=ORIENTED_EDGE ( 'NONE', *, *, #82795, .T. ) ;
#99301=ORIENTED_EDGE ( 'NONE', *, *, #136683, .T. ) ;
#99302=ADVANCED_FACE ( 'NONE', ( #48416 ), #136136, .F. ) ;
#99304=VERTEX_POINT ( 'NONE', #35446 ) ;
#99306=EDGE_CURVE ( 'NONE', #55371, #39920, #102816, .T. ) ;
#99307=VERTEX_POINT ( 'NONE', #45601 ) ;
#99310=ORIENTED_EDGE ( 'NONE', *, *, #101057, .T. ) ;
#99311=VECTOR ( 'NONE', #58414, 999.9999999999998863 ) ;
#99313=VECTOR ( 'NONE', #92346, 999.9999999999998863 ) ;
#99314=EDGE_CURVE ( 'NONE', #123801, #2587, #102100, .T. ) ;
#99315=CARTESIAN_POINT ( 'NONE',  ( -28.17183060077627133, 0.7592924766157034266, 4.000000000000000000 ) ) ;
#99317=FACE_OUTER_BOUND ( 'NONE', #8777, .T. ) ;
#99319=VERTEX_POINT ( 'NONE', #36821 ) ;
#99320=DIRECTION ( 'NONE',  ( -0.6830127018922180770, -0.6830127018922204085, -0.2588190451025213501 ) ) ;
#99321=CARTESIAN_POINT ( 'NONE',  ( -34.92500000000001137, 22.22500000000000142, 4.500000000000000888 ) ) ;
#99322=DIRECTION ( 'NONE',  ( 0.7071067811865486830, -0.7071067811865464625, -0.000000000000000000 ) ) ;
#99323=VECTOR ( 'NONE', #23733, 1000.000000000000000 ) ;
#99325=DIRECTION ( 'NONE',  ( -0.7071067811865486830, -0.7071067811865464625, 0.000000000000000000 ) ) ;
#99326=CARTESIAN_POINT ( 'NONE',  ( 14.99999999999989697, -12.41253812416062985, 4.000000000000000000 ) ) ;
#99328=LINE ( 'NONE', #22475, #24400 ) ;
#99329=FACE_OUTER_BOUND ( 'NONE', #110306, .T. ) ;
#99333=ORIENTED_EDGE ( 'NONE', *, *, #113497, .F. ) ;
#99335=DIRECTION ( 'NONE',  ( -0.7071067811865486830, -0.7071067811865464625, 0.000000000000000000 ) ) ;
#99336=CARTESIAN_POINT ( 'NONE',  ( 7.499999999999951150, -5.568876922607754132, 4.000000000000000000 ) ) ;
#99338=CARTESIAN_POINT ( 'NONE',  ( -22.49999999999984723, 14.14708470758589165, -0.5283514160166046247 ) ) ;
#99339=EDGE_CURVE ( 'NONE', #128576, #102869, #81797, .T. ) ;
#99340=DIRECTION ( 'NONE',  ( 0.7071067811865487940, 0.7071067811865463515, -0.000000000000000000 ) ) ;
#99343=EDGE_LOOP ( 'NONE', ( #17338, #601, #130770, #63823 ) ) ;
#99344=ORIENTED_EDGE ( 'NONE', *, *, #109856, .F. ) ;
#99345=DIRECTION ( 'NONE',  ( -0.6830127018922181881, 0.6830127018922202975, -0.2588190451025214056 ) ) ;
#99346=VERTEX_POINT ( 'NONE', #13624 ) ;
#99347=ORIENTED_EDGE ( 'NONE', *, *, #114521, .T. ) ;
#99349=ORIENTED_EDGE ( 'NONE', *, *, #120829, .T. ) ;
#99351=EDGE_CURVE ( 'NONE', #29293, #126178, #25228, .T. ) ;
#99352=LINE ( 'NONE', #121823, #57144 ) ;
#99353=CARTESIAN_POINT ( 'NONE',  ( -1.499999999999990896, 3.653845994658386331, -4.504631822206368597 ) ) ;
#99354=ADVANCED_FACE ( 'NONE', ( #69485 ), #26666, .F. ) ;
#99356=ORIENTED_EDGE ( 'NONE', *, *, #101420, .T. ) ;
#99357=DIRECTION ( 'NONE',  ( 0.3543493200069162685, -0.000000000000000000, -0.9351131265310288487 ) ) ;
#99358=ORIENTED_EDGE ( 'NONE', *, *, #126387, .T. ) ;
#99359=EDGE_LOOP ( 'NONE', ( #100927, #53433, #53096, #22555 ) ) ;
#99360=ORIENTED_EDGE ( 'NONE', *, *, #139986, .T. ) ;
#99362=DIRECTION ( 'NONE',  ( -0.000000000000000000, -0.3543493200069152693, 0.9351131265310292928 ) ) ;
#99363=ORIENTED_EDGE ( 'NONE', *, *, #52631, .T. ) ;
#99364=DIRECTION ( 'NONE',  ( -0.3543493200069162685, -0.000000000000000000, -0.9351131265310288487 ) ) ;
#99365=DIRECTION ( 'NONE',  ( 0.7071067811865486830, -0.7071067811865464625, -0.000000000000000000 ) ) ;
#99367=VECTOR ( 'NONE', #58314, 1000.000000000000000 ) ;
#99368=AXIS2_PLACEMENT_3D ( 'NONE', #12636, #68493, #110505 ) ;
#99370=DIRECTION ( 'NONE',  ( -0.7071067811865486830, -0.7071067811865464625, 0.000000000000000000 ) ) ;
#99371=AXIS2_PLACEMENT_3D ( 'NONE', #56325, #64297, #54865 ) ;
#99372=FACE_BOUND ( 'NONE', #93050, .T. ) ;
#99373=EDGE_LOOP ( 'NONE', ( #138801, #24348, #123354, #73818 ) ) ;
#99374=DIRECTION ( 'NONE',  ( 0.6830127018922181881, 0.6830127018922202975, -0.2588190451025214056 ) ) ;
#99375=LINE ( 'NONE', #89940, #39819 ) ;
#99376=FACE_OUTER_BOUND ( 'NONE', #35745, .T. ) ;
#99377=ORIENTED_EDGE ( 'NONE', *, *, #15984, .T. ) ;
#99378=DIRECTION ( 'NONE',  ( 0.7071067811865487940, 0.7071067811865463515, 0.000000000000000000 ) ) ;
#99379=ORIENTED_EDGE ( 'NONE', *, *, #34720, .T. ) ;
#99380=ORIENTED_EDGE ( 'NONE', *, *, #2570, .T. ) ;
#99381=VECTOR ( 'NONE', #86857, 1000.000000000000000 ) ;
#99386=DIRECTION ( 'NONE',  ( -0.7071067811865486830, 0.7071067811865464625, 0.000000000000000000 ) ) ;
#99387=CARTESIAN_POINT ( 'NONE',  ( -34.92500000000001137, 22.22500000000000142, 4.000000000000000000 ) ) ;
#99388=DIRECTION ( 'NONE',  ( -0.6830127018922180770, -0.6830127018922204085, -0.2588190451025213501 ) ) ;
#99390=DIRECTION ( 'NONE',  ( -0.7071067811865487940, 0.7071067811865463515, 0.000000000000000000 ) ) ;
#99391=DIRECTION ( 'NONE',  ( -0.7071067811865487940, 0.7071067811865463515, -0.000000000000000000 ) ) ;
#99393=VECTOR ( 'NONE', #1710, 1000.000000000000000 ) ;
#99394=AXIS2_PLACEMENT_3D ( 'NONE', #109687, #10355, #63369 ) ;
#99396=LINE ( 'NONE', #113137, #39341 ) ;
#99398=CARTESIAN_POINT ( 'NONE',  ( -27.32816939922333432, 5.259292476615663681, 4.000000000000000000 ) ) ;
#99399=DIRECTION ( 'NONE',  ( -0.000000000000000000, 0.000000000000000000, 1.000000000000000000 ) ) ;
#99400=EDGE_LOOP ( 'NONE', ( #65623, #30581, #13830, #119453 ) ) ;
#99401=EDGE_CURVE ( 'NONE', #6180, #61952, #134011, .T. ) ;
#99402=ORIENTED_EDGE ( 'NONE', *, *, #93774, .T. ) ;
#99404=AXIS2_PLACEMENT_3D ( 'NONE', #77811, #22663, #66933 ) ;
#99405=CARTESIAN_POINT ( 'NONE',  ( 30.29974487139158867, -27.71228299555227537, 4.000000000000000000 ) ) ;
#99406=DIRECTION ( 'NONE',  ( -0.000000000000000000, 0.3543493200069153248, 0.9351131265310292928 ) ) ;
#99407=ORIENTED_EDGE ( 'NONE', *, *, #42565, .F. ) ;
#99408=VECTOR ( 'NONE', #7482, 999.9999999999998863 ) ;
#99409=VECTOR ( 'NONE', #133393, 1000.000000000000000 ) ;
#99410=VERTEX_POINT ( 'NONE', #2009 ) ;
#99412=CARTESIAN_POINT ( 'NONE',  ( -24.48921356237309510, -27.52281430457072631, 5.000000000000000000 ) ) ;
#99413=EDGE_CURVE ( 'NONE', #66330, #23113, #90508, .T. ) ;
#99414=ADVANCED_FACE ( 'NONE', ( #39712 ), #83194, .T. ) ;
#99415=DIRECTION ( 'NONE',  ( -0.7071067811865486830, -0.7071067811865464625, -0.000000000000000000 ) ) ;
#99416=VERTEX_POINT ( 'NONE', #84625 ) ;
#99417=AXIS2_PLACEMENT_3D ( 'NONE', #134315, #87937, #32875 ) ;
#99418=CARTESIAN_POINT ( 'NONE',  ( -8.331532588401378447, -18.74070752338409207, 20.73178291233839232 ) ) ;
#99419=CARTESIAN_POINT ( 'NONE',  ( 5.994519915287488843, 28.92564299267942118, 4.000000000000000000 ) ) ;
#99420=EDGE_CURVE ( 'NONE', #103007, #22844, #127396, .T. ) ;
#99421=EDGE_CURVE ( 'NONE', #126872, #62368, #71610, .T. ) ;
#99423=DIRECTION ( 'NONE',  ( 0.7071067811865487940, 0.7071067811865463515, 0.000000000000000000 ) ) ;
#99424=EDGE_CURVE ( 'NONE', #9261, #67480, #96178, .T. ) ;
#99425=VERTEX_POINT ( 'NONE', #72363 ) ;
#99428=LINE ( 'NONE', #85706, #32679 ) ;
#99429=CARTESIAN_POINT ( 'NONE',  ( 31.82816939922331656, -20.24070752338406720, 4.000000000000000000 ) ) ;
#99430=VECTOR ( 'NONE', #114805, 1000.000000000000000 ) ;
#99431=CARTESIAN_POINT ( 'NONE',  ( 7.499999999999951150, 3.073033219394630144, -6.593910359670951848 ) ) ;
#99435=EDGE_CURVE ( 'NONE', #123251, #127158, #139744, .T. ) ;
#99436=CARTESIAN_POINT ( 'NONE',  ( -34.92500000000001137, -20.33753812416080820, 4.000000000000000000 ) ) ;
#99437=LINE ( 'NONE', #43654, #30794 ) ;
#99439=ORIENTED_EDGE ( 'NONE', *, *, #58131, .T. ) ;
#99440=EDGE_CURVE ( 'NONE', #32541, #105769, #137579, .T. ) ;
#99441=CARTESIAN_POINT ( 'NONE',  ( -44.99451991528749772, 28.92564299267969474, 4.000000000000000000 ) ) ;
#99443=VERTEX_POINT ( 'NONE', #107075 ) ;
#99444=CARTESIAN_POINT ( 'NONE',  ( 15.18398860626900237, 28.73617430169797871, 5.000000000000000000 ) ) ;
#99445=CARTESIAN_POINT ( 'NONE',  ( 36.48921356237310221, -27.52281430457080802, 5.000000000000000000 ) ) ;
#99446=ORIENTED_EDGE ( 'NONE', *, *, #142523, .F. ) ;
#99447=ADVANCED_FACE ( 'NONE', ( #7005 ), #4861, .F. ) ;
#99448=DIRECTION ( 'NONE',  ( -0.7071067811865486830, -0.7071067811865464625, 0.000000000000000000 ) ) ;
#99449=CARTESIAN_POINT ( 'NONE',  ( -9.005480084712511157, 28.92564299267931816, 4.000000000000000000 ) ) ;
#99451=ORIENTED_EDGE ( 'NONE', *, *, #3784, .T. ) ;
#99453=CARTESIAN_POINT ( 'NONE',  ( 32.99999999999977263, -2.904428200921273184, -6.989807076075017278 ) ) ;
#99455=ORIENTED_EDGE ( 'NONE', *, *, #59423, .F. ) ;
#99456=DIRECTION ( 'NONE',  ( 0.7071067811865487940, 0.7071067811865463515, -0.000000000000000000 ) ) ;
#99457=CARTESIAN_POINT ( 'NONE',  ( 30.18398860626900060, 28.73617430169808173, 5.000000000000000000 ) ) ;
#99458=CARTESIAN_POINT ( 'NONE',  ( 27.61838490601979146, -2.240707523384260824, 13.37739548510232979 ) ) ;
#99459=ORIENTED_EDGE ( 'NONE', *, *, #46468, .F. ) ;
#99460=FACE_OUTER_BOUND ( 'NONE', #8186, .T. ) ;
#99461=DIRECTION ( 'NONE',  ( 0.7071067811865487940, 0.7071067811865463515, -0.000000000000000000 ) ) ;
#99462=DIRECTION ( 'NONE',  ( -0.7071067811865486830, -0.7071067811865464625, 0.000000000000000000 ) ) ;
#99465=CARTESIAN_POINT ( 'NONE',  ( -60.29974487139158867, -27.71228299555248142, 4.000000000000000000 ) ) ;
#99467=ORIENTED_EDGE ( 'NONE', *, *, #108237, .F. ) ;
#99468=EDGE_CURVE ( 'NONE', #109300, #134825, #117917, .T. ) ;
#99469=CARTESIAN_POINT ( 'NONE',  ( 9.183988606268997046, 28.73617430169793607, 5.000000000000000000 ) ) ;
#99470=ORIENTED_EDGE ( 'NONE', *, *, #5232, .T. ) ;
#99471=EDGE_CURVE ( 'NONE', #20421, #871, #60774, .T. ) ;
#99472=EDGE_LOOP ( 'NONE', ( #130728, #121751, #81526, #26176 ) ) ;
#99473=DIRECTION ( 'NONE',  ( -0.000000000000000000, -0.000000000000000000, 1.000000000000000000 ) ) ;
#99474=DIRECTION ( 'NONE',  ( 1.000000000000000000, 0.000000000000000000, 0.000000000000000000 ) ) ;
#99476=VECTOR ( 'NONE', #128277, 1000.000000000000000 ) ;
#99477=ORIENTED_EDGE ( 'NONE', *, *, #17637, .T. ) ;
#99478=EDGE_CURVE ( 'NONE', #98566, #105535, #16476, .T. ) ;
#99480=CARTESIAN_POINT ( 'NONE',  ( -14.99999999999988809, 17.96639925780207747, 5.000000000000000000 ) ) ;
#99481=VECTOR ( 'NONE', #117578, 1000.000000000000000 ) ;
#99482=DIRECTION ( 'NONE',  ( 0.7071067811865487940, 0.7071067811865463515, 0.000000000000000000 ) ) ;
#99483=DIRECTION ( 'NONE',  ( -0.7071067811865486830, -0.7071067811865464625, -0.000000000000000000 ) ) ;
#99485=VERTEX_POINT ( 'NONE', #49869 ) ;
#99486=CARTESIAN_POINT ( 'NONE',  ( -30.48921356237309510, -27.52281430457076894, 5.000000000000000000 ) ) ;
#99487=CARTESIAN_POINT ( 'NONE',  ( 10.49999999999993250, 1.030536316426522436, -5.498701923753822385 ) ) ;
#99488=VECTOR ( 'NONE', #32312, 1000.000000000000000 ) ;
#99492=DIRECTION ( 'NONE',  ( -0.000000000000000000, 0.000000000000000000, 1.000000000000000000 ) ) ;
#99494=CARTESIAN_POINT ( 'NONE',  ( -33.29974487139158867, -27.71228299555229313, 4.000000000000000000 ) ) ;
#99495=CARTESIAN_POINT ( 'NONE',  ( 9.299744871391588674, -27.71228299555212971, 4.000000000000000000 ) ) ;
#99496=AXIS2_PLACEMENT_3D ( 'NONE', #98054, #76307, #42974 ) ;
#99497=ORIENTED_EDGE ( 'NONE', *, *, #59788, .T. ) ;
#99498=VERTEX_POINT ( 'NONE', #73061 ) ;
#99500=ADVANCED_FACE ( 'NONE', ( #83941 ), #128141, .F. ) ;
#99501=CARTESIAN_POINT ( 'NONE',  ( -16.49999999999988276, 13.08746187583911436, 4.000000000000000000 ) ) ;
#99502=VECTOR ( 'NONE', #49450, 1000.000000000000000 ) ;
#99503=AXIS2_PLACEMENT_3D ( 'NONE', #89941, #33475, #77675 ) ;
#99505=VERTEX_POINT ( 'NONE', #131700 ) ;
#99506=CARTESIAN_POINT ( 'NONE',  ( 41.99451991528749062, 28.92564299267967343, 4.000000000000000000 ) ) ;
#99507=VECTOR ( 'NONE', #88141, 999.9999999999998863 ) ;
#99510=EDGE_LOOP ( 'NONE', ( #76062, #126488, #50456, #143430 ) ) ;
#99511=CARTESIAN_POINT ( 'NONE',  ( -27.18398860626900060, 28.73617430169806042, 5.000000000000000000 ) ) ;
#99512=ORIENTED_EDGE ( 'NONE', *, *, #49810, .T. ) ;
#99513=VERTEX_POINT ( 'NONE', #41829 ) ;
#99514=PLANE ( 'NONE',  #132878 ) ;
#99515=AXIS2_PLACEMENT_3D ( 'NONE', #114156, #101855, #69992 ) ;
#99517=DIRECTION ( 'NONE',  ( -0.7071067811865486830, -0.7071067811865464625, 0.000000000000000000 ) ) ;
#99518=LINE ( 'NONE', #10373, #32789 ) ;
#99519=CARTESIAN_POINT ( 'NONE',  ( -15.18398860626900237, 28.73617430169797871, 5.000000000000000000 ) ) ;
#99520=VERTEX_POINT ( 'NONE', #88932 ) ;
#99521=ADVANCED_FACE ( 'NONE', ( #86052 ), #99770, .F. ) ;
#99522=CARTESIAN_POINT ( 'NONE',  ( 9.489213562373095101, -27.52281430457062328, 5.000000000000000000 ) ) ;
#99523=VERTEX_POINT ( 'NONE', #120058 ) ;
#99524=AXIS2_PLACEMENT_3D ( 'NONE', #112918, #23019, #569 ) ;
#99527=LINE ( 'NONE', #122728, #96384 ) ;
#99528=FACE_OUTER_BOUND ( 'NONE', #114993, .T. ) ;
#99529=VECTOR ( 'NONE', #134690, 999.9999999999998863 ) ;
#99530=FACE_OUTER_BOUND ( 'NONE', #21096, .T. ) ;
#99531=DIRECTION ( 'NONE',  ( 1.000000000000000000, 0.000000000000000000, 0.000000000000000000 ) ) ;
#99532=ORIENTED_EDGE ( 'NONE', *, *, #62378, .T. ) ;
#99533=VECTOR ( 'NONE', #101727, 999.9999999999998863 ) ;
#99534=DIRECTION ( 'NONE',  ( 0.7071067811865487940, 0.7071067811865463515, 0.000000000000000000 ) ) ;
#99536=CARTESIAN_POINT ( 'NONE',  ( -24.98480450340313652, 2.536990198832462351, 5.000000000000000000 ) ) ;
#99537=LINE ( 'NONE', #56821, #107972 ) ;
#99538=CARTESIAN_POINT ( 'NONE',  ( 34.42499999999998295, 7.541399257801974620, 5.000000000000000000 ) ) ;
#99539=ORIENTED_EDGE ( 'NONE', *, *, #18605, .T. ) ;
#99540=ORIENTED_EDGE ( 'NONE', *, *, #80488, .F. ) ;
#99541=AXIS2_PLACEMENT_3D ( 'NONE', #21233, #111069, #89347 ) ;
#99542=CARTESIAN_POINT ( 'NONE',  ( 11.99999999999991296, 1.931123077392161935, 4.000000000000000000 ) ) ;
#99543=ORIENTED_EDGE ( 'NONE', *, *, #94309, .F. ) ;
#99544=ADVANCED_FACE ( 'NONE', ( #121514 ), #65771, .T. ) ;
#99546=FACE_OUTER_BOUND ( 'NONE', #100313, .T. ) ;
#99548=DIRECTION ( 'NONE',  ( 0.7071067811865487940, -0.7071067811865463515, 0.000000000000000000 ) ) ;
#99549=DIRECTION ( 'NONE',  ( 0.6830127018922180770, -0.6830127018922204085, -0.2588190451025213501 ) ) ;
#99550=DIRECTION ( 'NONE',  ( 0.7071067811865487940, 0.7071067811865463515, 0.000000000000000000 ) ) ;
#99551=AXIS2_PLACEMENT_3D ( 'NONE', #31346, #20436, #42948 ) ;
#99552=DIRECTION ( 'NONE',  ( 0.6830127018922181881, 0.6830127018922202975, -0.2588190451025214056 ) ) ;
#99553=FACE_BOUND ( 'NONE', #85953, .T. ) ;
#99554=EDGE_CURVE ( 'NONE', #131602, #65100, #97622, .T. ) ;
#99555=PLANE ( 'NONE',  #64117 ) ;
#99556=CARTESIAN_POINT ( 'NONE',  ( 17.29289321881333663, 14.25929247661557397, 5.000000000000000000 ) ) ;
#99557=LINE ( 'NONE', #100999, #10914 ) ;
#99559=ORIENTED_EDGE ( 'NONE', *, *, #364, .F. ) ;
#99560=VECTOR ( 'NONE', #88102, 1000.000000000000000 ) ;
#99561=PLANE ( 'NONE',  #39457 ) ;
#99562=ORIENTED_EDGE ( 'NONE', *, *, #52204, .F. ) ;
#99563=ORIENTED_EDGE ( 'NONE', *, *, #135634, .T. ) ;
#99565=VERTEX_POINT ( 'NONE', #118670 ) ;
#99566=LINE ( 'NONE', #240, #126337 ) ;
#99567=DIRECTION ( 'NONE',  ( -0.7071067811865486830, -0.7071067811865464625, 0.000000000000000000 ) ) ;
#99568=ORIENTED_EDGE ( 'NONE', *, *, #37252, .T. ) ;
#99569=CARTESIAN_POINT ( 'NONE',  ( -34.92500000000002558, 18.75929247661552424, 4.255531930566273324 ) ) ;
#99570=CARTESIAN_POINT ( 'NONE',  ( -10.49999999999993250, -1.592773361805382981, -6.492772025301205119 ) ) ;
#99573=CARTESIAN_POINT ( 'NONE',  ( -18.48921356237309510, -27.52281430457068367, 5.000000000000000000 ) ) ;
#99575=CARTESIAN_POINT ( 'NONE',  ( -26.67183060077628554, 17.25929247661554200, 4.000000000000000000 ) ) ;
#99578=VECTOR ( 'NONE', #26289, 1000.000000000000000 ) ;
#99579=EDGE_LOOP ( 'NONE', ( #75057, #63601, #100298, #132662 ) ) ;
#99580=VECTOR ( 'NONE', #68127, 1000.000000000000000 ) ;
#99581=VECTOR ( 'NONE', #92148, 1000.000000000000000 ) ;
#99582=VECTOR ( 'NONE', #31896, 999.9999999999998863 ) ;
#99583=VERTEX_POINT ( 'NONE', #133149 ) ;
#99584=CARTESIAN_POINT ( 'NONE',  ( 31.17183060077625711, -14.24070752338414003, 4.000000000000000000 ) ) ;
#99585=DIRECTION ( 'NONE',  ( -0.7071067811865487940, 0.7071067811865463515, -0.000000000000000000 ) ) ;
#99587=ORIENTED_EDGE ( 'NONE', *, *, #127956, .T. ) ;
#99591=ORIENTED_EDGE ( 'NONE', *, *, #52529, .T. ) ;
#99592=VECTOR ( 'NONE', #102222, 1000.000000000000227 ) ;
#99593=CARTESIAN_POINT ( 'NONE',  ( -22.49999999999984013, -5.568876922607759461, 4.000000000000000000 ) ) ;
#99595=EDGE_CURVE ( 'NONE', #98842, #82613, #20777, .T. ) ;
#99599=EDGE_LOOP ( 'NONE', ( #6873, #21462, #34837, #5817 ) ) ;
#99600=DIRECTION ( 'NONE',  ( -0.6830127018922180770, -0.6830127018922204085, -0.2588190451025213501 ) ) ;
#99601=EDGE_CURVE ( 'NONE', #86268, #6488, #75200, .T. ) ;
#99605=DIRECTION ( 'NONE',  ( -0.6830127018922181881, 0.6830127018922202975, -0.2588190451025214056 ) ) ;
#99606=DIRECTION ( 'NONE',  ( -0.7071067811865487940, 0.7071067811865463515, 0.000000000000000000 ) ) ;
#99609=EDGE_CURVE ( 'NONE', #31236, #4046, #96876, .T. ) ;
#99610=DIRECTION ( 'NONE',  ( 0.7071067811865487940, 0.7071067811865463515, -0.000000000000000000 ) ) ;
#99611=LINE ( 'NONE', #109793, #127871 ) ;
#99612=DIRECTION ( 'NONE',  ( -0.7071067811865487940, 0.7071067811865463515, -0.000000000000000000 ) ) ;
#99613=ORIENTED_EDGE ( 'NONE', *, *, #66263, .T. ) ;
#99614=AXIS2_PLACEMENT_3D ( 'NONE', #80671, #89384, #67675 ) ;
#99615=DIRECTION ( 'NONE',  ( -0.000000000000000000, 0.000000000000000000, 1.000000000000000000 ) ) ;
#99616=VECTOR ( 'NONE', #66797, 1000.000000000000000 ) ;
#99617=VERTEX_POINT ( 'NONE', #141122 ) ;
#99618=EDGE_CURVE ( 'NONE', #16747, #42386, #109934, .T. ) ;
#99619=AXIS2_PLACEMENT_3D ( 'NONE', #133062, #77948, #11948 ) ;
#99620=DIRECTION ( 'NONE',  ( 0.7071067811865487940, 0.7071067811865463515, 0.000000000000000000 ) ) ;
#99622=CARTESIAN_POINT ( 'NONE',  ( 69.18398860626899705, 28.73617430169835529, 5.000000000000000000 ) ) ;
#99623=CARTESIAN_POINT ( 'NONE',  ( -63.48921356237309510, -27.52281430457099631, 5.000000000000000000 ) ) ;
#99624=VECTOR ( 'NONE', #43166, 999.9999999999998863 ) ;
#99626=DIRECTION ( 'NONE',  ( -0.7071067811865486830, -0.7071067811865464625, 0.000000000000000000 ) ) ;
#99627=ADVANCED_FACE ( 'NONE', ( #108464 ), #143277, .F. ) ;
#99628=DIRECTION ( 'NONE',  ( 0.7071067811865487940, 0.7071067811865463515, 0.000000000000000000 ) ) ;
#99630=EDGE_CURVE ( 'NONE', #76459, #37329, #47585, .T. ) ;
#99631=EDGE_LOOP ( 'NONE', ( #127297, #42404, #13503, #26890 ) ) ;
#99632=VECTOR ( 'NONE', #48302, 1000.000000000000114 ) ;
#99633=DIRECTION ( 'NONE',  ( 0.7071067811865486830, -0.7071067811865464625, -0.000000000000000000 ) ) ;
#99634=ORIENTED_EDGE ( 'NONE', *, *, #116768, .T. ) ;
#99635=LINE ( 'NONE', #22074, #23911 ) ;
#99636=EDGE_CURVE ( 'NONE', #68994, #8228, #90320, .T. ) ;
#99638=CARTESIAN_POINT ( 'NONE',  ( -15.32816939922342314, 14.25929247661557042, 4.000000000000000000 ) ) ;
#99640=VECTOR ( 'NONE', #108917, 1000.000000000000000 ) ;
#99641=CARTESIAN_POINT ( 'NONE',  ( 22.49999999999984723, -7.533600742197665845, 5.000000000000000000 ) ) ;
#99642=LINE ( 'NONE', #44615, #4755 ) ;
#99643=CARTESIAN_POINT ( 'NONE',  ( 20.99451991528748707, 28.92564299267952777, 4.000000000000000000 ) ) ;
#99644=VERTEX_POINT ( 'NONE', #80894 ) ;
#99645=CARTESIAN_POINT ( 'NONE',  ( -34.49999999999975842, -10.04351517176480613, -1.623559851933904508 ) ) ;
#99646=CARTESIAN_POINT ( 'NONE',  ( 19.82816939922339827, 18.75929247661552424, 4.000000000000000000 ) ) ;
#99647=VECTOR ( 'NONE', #14477, 1000.000000000000114 ) ;
#99648=DIRECTION ( 'NONE',  ( -0.000000000000000000, -0.3543493200069152693, 0.9351131265310292928 ) ) ;
#99650=CARTESIAN_POINT ( 'NONE',  ( 23.03315071937583980, 7.620612595215163765, 4.000000000000000000 ) ) ;
#99652=CARTESIAN_POINT ( 'NONE',  ( -54.48921356237310221, -27.52281430457093236, 5.000000000000000000 ) ) ;
#99654=CARTESIAN_POINT ( 'NONE',  ( -23.29289321881329755, -18.74070752338409207, 5.000000000000000000 ) ) ;
#99656=LINE ( 'NONE', #77937, #9417 ) ;
#99657=ORIENTED_EDGE ( 'NONE', *, *, #50507, .T. ) ;
#99660=ORIENTED_EDGE ( 'NONE', *, *, #56265, .T. ) ;
#99662=LINE ( 'NONE', #120696, #45498 ) ;
#99663=CARTESIAN_POINT ( 'NONE',  ( 6.707013264292989163, -21.74070752338407075, 4.999753212805213565 ) ) ;
#99664=LINE ( 'NONE', #43176, #129443 ) ;
#99665=DIRECTION ( 'NONE',  ( -0.7071067811865486830, -0.7071067811865464625, 0.000000000000000000 ) ) ;
#99667=CARTESIAN_POINT ( 'NONE',  ( -34.42500000000001137, -22.22500000000000142, 5.000000000000000000 ) ) ;
#99668=FACE_OUTER_BOUND ( 'NONE', #91122, .T. ) ;
#99669=ORIENTED_EDGE ( 'NONE', *, *, #143334, .F. ) ;
#99670=VERTEX_POINT ( 'NONE', #24355 ) ;
#99671=CARTESIAN_POINT ( 'NONE',  ( 18.48921356237309510, -27.52281430457068367, 5.000000000000000000 ) ) ;
#99672=DIRECTION ( 'NONE',  ( -0.6830127018922180770, -0.6830127018922204085, -0.2588190451025213501 ) ) ;
#99674=AXIS2_PLACEMENT_3D ( 'NONE', #126215, #92134, #136364 ) ;
#99675=CARTESIAN_POINT ( 'NONE',  ( -32.99999999999976552, -1.068876922607802538, 4.000000000000000000 ) ) ;
#99676=EDGE_CURVE ( 'NONE', #89784, #50446, #123701, .T. ) ;
#99677=CARTESIAN_POINT ( 'NONE',  ( -18.48921356237309510, -27.52281430457068367, 5.000000000000000000 ) ) ;
#99679=PLANE ( 'NONE',  #25512 ) ;
#99680=DIRECTION ( 'NONE',  ( -0.6830127018922181881, 0.6830127018922202975, -0.2588190451025214056 ) ) ;
#99681=ORIENTED_EDGE ( 'NONE', *, *, #4165, .F. ) ;
#99682=( BOUNDED_CURVE ( )  B_SPLINE_CURVE ( 3, ( #5278, #137977, #93749, #104616 ),
 .UNSPECIFIED., .F., .T. ) 
 B_SPLINE_CURVE_WITH_KNOTS ( ( 4, 4 ),
 ( 2.001653308786158547, 3.503810798801450854 ),
 .UNSPECIFIED. ) 
 CURVE ( )  GEOMETRIC_REPRESENTATION_ITEM ( )  RATIONAL_B_SPLINE_CURVE ( ( 1.000000000000000000, 0.8206354192515217250, 0.8206354192515217250, 1.000000000000000000 ) ) 
 REPRESENTATION_ITEM ( '' )  );
#99684=PLANE ( 'NONE',  #30763 ) ;
#99686=LINE ( 'NONE', #12675, #127271 ) ;
#99687=LINE ( 'NONE', #34446, #105319 ) ;
#99688=ORIENTED_EDGE ( 'NONE', *, *, #112592, .T. ) ;
#99690=CARTESIAN_POINT ( 'NONE',  ( 0.000000000000000000, 0.000000000000000000, 5.000000000000000000 ) ) ;
#99691=VECTOR ( 'NONE', #61638, 1000.000000000000000 ) ;
#99692=ORIENTED_EDGE ( 'NONE', *, *, #97854, .F. ) ;
#99693=VECTOR ( 'NONE', #75680, 1000.000000000000227 ) ;
#99694=EDGE_CURVE ( 'NONE', #18830, #102325, #101196, .T. ) ;
#99695=CARTESIAN_POINT ( 'NONE',  ( 50.99451991528749062, 28.92564299267973738, 4.000000000000000000 ) ) ;
#99697=DIRECTION ( 'NONE',  ( 0.7071067811865487940, 0.7071067811865463515, -0.000000000000000000 ) ) ;
#99698=VERTEX_POINT ( 'NONE', #68601 ) ;
#99700=VECTOR ( 'NONE', #117288, 1000.000000000000000 ) ;
#99701=VECTOR ( 'NONE', #14946, 1000.000000000000000 ) ;
#99702=AXIS2_PLACEMENT_3D ( 'NONE', #65655, #54053, #43154 ) ;
#99704=LINE ( 'NONE', #106446, #54543 ) ;
#99705=CARTESIAN_POINT ( 'NONE',  ( -29.00492477221176557, -5.240707523384228850, 12.38332538355502699 ) ) ;
#99706=DIRECTION ( 'NONE',  ( 0.6830127018922181881, 0.6830127018922202975, -0.2588190451025214056 ) ) ;
#99707=EDGE_CURVE ( 'NONE', #21499, #119750, #112787, .T. ) ;
#99709=CARTESIAN_POINT ( 'NONE',  ( 13.49999999999990052, -12.66682484999665093, -0.6294897503863620125 ) ) ;
#99713=CARTESIAN_POINT ( 'NONE',  ( 35.99451991528749772, 28.92564299267963079, 4.000000000000000000 ) ) ;
#99714=AXIS2_PLACEMENT_3D ( 'NONE', #67271, #57132, #46996 ) ;
#99715=CARTESIAN_POINT ( 'NONE',  ( 60.48921356237309510, -27.52281430457097500, 5.000000000000000000 ) ) ;
#99716=VERTEX_POINT ( 'NONE', #22893 ) ;
#99717=EDGE_LOOP ( 'NONE', ( #105125, #58524, #32274, #86899 ) ) ;
#99720=AXIS2_PLACEMENT_3D ( 'NONE', #87098, #65376, #132043 ) ;
#99721=FACE_OUTER_BOUND ( 'NONE', #34192, .T. ) ;
#99722=LINE ( 'NONE', #123657, #135992 ) ;
#99723=AXIS2_PLACEMENT_3D ( 'NONE', #27996, #136739, #115670 ) ;
#99724=CARTESIAN_POINT ( 'NONE',  ( 15.79333936457837062, 21.75929247661549937, 4.998822639870715179 ) ) ;
#99725=LINE ( 'NONE', #43232, #142775 ) ;
#99727=VERTEX_POINT ( 'NONE', #69307 ) ;
#99730=ADVANCED_FACE ( 'NONE', ( #58478 ), #3970, .F. ) ;
#99731=VECTOR ( 'NONE', #133988, 1000.000000000000000 ) ;
#99733=VECTOR ( 'NONE', #95966, 1000.000000000000227 ) ;
#99735=PLANE ( 'NONE',  #25950 ) ;
#99736=VECTOR ( 'NONE', #66893, 1000.000000000000114 ) ;
#99738=FACE_OUTER_BOUND ( 'NONE', #133410, .T. ) ;
#99741=FACE_BOUND ( 'NONE', #14400, .T. ) ;
#99742=VECTOR ( 'NONE', #94480, 1000.000000000000000 ) ;
#99743=ADVANCED_FACE ( 'NONE', ( #12042 ), #101918, .T. ) ;
#99744=CARTESIAN_POINT ( 'NONE',  ( -14.20710678118644488, -20.24070752338407431, 5.000000000000000000 ) ) ;
#99746=DIRECTION ( 'NONE',  ( 0.3543493200069162685, -0.000000000000000000, -0.9351131265310288487 ) ) ;
#99747=LINE ( 'NONE', #141100, #122158 ) ;
#99749=ORIENTED_EDGE ( 'NONE', *, *, #108340, .F. ) ;
#99750=VECTOR ( 'NONE', #58369, 999.9999999999998863 ) ;
#99751=EDGE_LOOP ( 'NONE', ( #21752, #19149, #141305, #86933 ) ) ;
#99754=DIRECTION ( 'NONE',  ( 1.000000000000000000, 0.000000000000000000, 0.000000000000000000 ) ) ;
#99755=ORIENTED_EDGE ( 'NONE', *, *, #16485, .T. ) ;
#99757=PLANE ( 'NONE',  #42353 ) ;
#99758=VECTOR ( 'NONE', #92684, 1000.000000000000000 ) ;
#99759=EDGE_CURVE ( 'NONE', #78430, #90132, #1834, .T. ) ;
#99760=CARTESIAN_POINT ( 'NONE',  ( 14.81601139373099585, 28.73617430169776910, 5.000000000000000000 ) ) ;
#99761=LINE ( 'NONE', #432, #111977 ) ;
#99762=VERTEX_POINT ( 'NONE', #36650 ) ;
#99763=CARTESIAN_POINT ( 'NONE',  ( 57.18398860626899705, 28.73617430169827358, 5.000000000000000000 ) ) ;
#99764=CARTESIAN_POINT ( 'NONE',  ( -38.20003122016812824, 8.259292476615641476, 16.85664084051850509 ) ) ;
#99765=DIRECTION ( 'NONE',  ( 0.000000000000000000, 0.000000000000000000, -1.000000000000000000 ) ) ;
#99766=LINE ( 'NONE', #46135, #31877 ) ;
#99767=DIRECTION ( 'NONE',  ( -0.7071067811865486830, -0.7071067811865464625, 0.000000000000000000 ) ) ;
#99768=DIRECTION ( 'NONE',  ( -0.7071067811865486830, -0.7071067811865464625, 0.000000000000000000 ) ) ;
#99769=AXIS2_PLACEMENT_3D ( 'NONE', #22930, #45470, #21547 ) ;
#99770=PLANE ( 'NONE',  #25949 ) ;
#99771=VERTEX_POINT ( 'NONE', #103320 ) ;
#99773=FACE_OUTER_BOUND ( 'NONE', #93261, .T. ) ;
#99774=ORIENTED_EDGE ( 'NONE', *, *, #35243, .F. ) ;
#99775=VERTEX_POINT ( 'NONE', #135972 ) ;
#99778=VECTOR ( 'NONE', #128416, 1000.000000000000000 ) ;
#99780=FACE_OUTER_BOUND ( 'NONE', #4169, .T. ) ;
#99781=EDGE_CURVE ( 'NONE', #132715, #8240, #46892, .T. ) ;
#99784=DIRECTION ( 'NONE',  ( 1.000000000000000000, 0.000000000000000000, 0.000000000000000000 ) ) ;
#99785=EDGE_CURVE ( 'NONE', #20021, #41454, #89608, .T. ) ;
#99787=CARTESIAN_POINT ( 'NONE',  ( 34.92499999999998295, -21.72500000000000142, 5.000000000000000000 ) ) ;
#99788=VECTOR ( 'NONE', #103703, 1000.000000000000000 ) ;
#99789=DIRECTION ( 'NONE',  ( -0.3543493200069162685, -0.000000000000000000, -0.9351131265310288487 ) ) ;
#99790=EDGE_CURVE ( 'NONE', #42222, #82630, #91070, .T. ) ;
#99792=DIRECTION ( 'NONE',  ( 0.7071067811865487940, -0.7071067811865463515, 0.000000000000000000 ) ) ;
#99795=VECTOR ( 'NONE', #123127, 1000.000000000000000 ) ;
#99796=VERTEX_POINT ( 'NONE', #14897 ) ;
#99797=CARTESIAN_POINT ( 'NONE',  ( 0.000000000000000000, 0.000000000000000000, 5.000000000000000000 ) ) ;
#99798=DIRECTION ( 'NONE',  ( 0.6830127018922181881, 0.6830127018922202975, -0.2588190451025214056 ) ) ;
#99799=ORIENTED_EDGE ( 'NONE', *, *, #21897, .T. ) ;
#99801=VERTEX_POINT ( 'NONE', #59854 ) ;
#99802=EDGE_LOOP ( 'NONE', ( #43570, #112435, #80156, #17434 ) ) ;
#99804=VECTOR ( 'NONE', #126732, 1000.000000000000000 ) ;
#99805=VECTOR ( 'NONE', #93797, 1000.000000000000000 ) ;
#99806=VECTOR ( 'NONE', #6184, 1000.000000000000000 ) ;
#99808=AXIS2_PLACEMENT_3D ( 'NONE', #111947, #80752, #123557 ) ;
#99809=FACE_OUTER_BOUND ( 'NONE', #94297, .T. ) ;
#99810=EDGE_CURVE ( 'NONE', #13309, #101471, #26503, .T. ) ;
#99811=DIRECTION ( 'NONE',  ( 0.7071067811865487940, 0.7071067811865463515, 0.000000000000000000 ) ) ;
#99812=EDGE_CURVE ( 'NONE', #13717, #5851, #83030, .T. ) ;
#99813=ORIENTED_EDGE ( 'NONE', *, *, #115798, .T. ) ;
#99815=DIRECTION ( 'NONE',  ( -0.7071067811865486830, -0.7071067811865464625, 0.000000000000000000 ) ) ;
#99816=VECTOR ( 'NONE', #131810, 1000.000000000000000 ) ;
#99817=ORIENTED_EDGE ( 'NONE', *, *, #75077, .T. ) ;
#99818=ADVANCED_FACE ( 'NONE', ( #70749 ), #51837, .F. ) ;
#99820=LINE ( 'NONE', #10643, #92548 ) ;
#99821=LINE ( 'NONE', #99079, #115399 ) ;
#99824=VERTEX_POINT ( 'NONE', #62719 ) ;
#99825=VERTEX_POINT ( 'NONE', #27199 ) ;
#99827=FACE_OUTER_BOUND ( 'NONE', #28311, .T. ) ;
#99828=CARTESIAN_POINT ( 'NONE',  ( -42.18398860626899705, 28.73617430169816700, 5.000000000000000000 ) ) ;
#99829=EDGE_CURVE ( 'NONE', #75799, #106339, #49197, .T. ) ;
#99833=AXIS2_PLACEMENT_3D ( 'NONE', #120195, #109360, #11440 ) ;
#99834=CARTESIAN_POINT ( 'NONE',  ( -14.54487008052910824, -0.7407075233842735917, 4.335043535661659675 ) ) ;
#99835=CARTESIAN_POINT ( 'NONE',  ( 21.79289321881330821, -2.240707523384255939, 5.000000000000000000 ) ) ;
#99836=CARTESIAN_POINT ( 'NONE',  ( 19.41932091537965732, -22.22500000000000142, -15.59309469223181210 ) ) ;
#99837=CARTESIAN_POINT ( 'NONE',  ( -27.32816939922334853, 11.25929247661560062, 4.000000000000000000 ) ) ;
#99838=VECTOR ( 'NONE', #84638, 1000.000000000000000 ) ;
#99840=DIRECTION ( 'NONE',  ( -1.000000000000000000, 0.000000000000000000, 0.000000000000000000 ) ) ;
#99841=EDGE_CURVE ( 'NONE', #88480, #78244, #116367, .T. ) ;
#99843=CARTESIAN_POINT ( 'NONE',  ( -20.99999999999985079, -21.03360074219752462, 5.000000000000000000 ) ) ;
#99845=ORIENTED_EDGE ( 'NONE', *, *, #110640, .T. ) ;
#99846=FACE_OUTER_BOUND ( 'NONE', #10734, .T. ) ;
#99847=FACE_OUTER_BOUND ( 'NONE', #55346, .T. ) ;
#99848=ORIENTED_EDGE ( 'NONE', *, *, #97654, .T. ) ;
#99849=AXIS2_PLACEMENT_3D ( 'NONE', #54421, #121061, #21764 ) ;
#99851=DIRECTION ( 'NONE',  ( -0.000000000000000000, 0.3543493200069153248, 0.9351131265310292928 ) ) ;
#99852=ORIENTED_EDGE ( 'NONE', *, *, #74200, .T. ) ;
#99853=DIRECTION ( 'NONE',  ( -0.7071067811865487940, 0.7071067811865463515, -0.000000000000000000 ) ) ;
#99854=ORIENTED_EDGE ( 'NONE', *, *, #91236, .T. ) ;
#99855=DIRECTION ( 'NONE',  ( 0.7071067811865486830, -0.7071067811865464625, -0.000000000000000000 ) ) ;
#99856=ORIENTED_EDGE ( 'NONE', *, *, #138484, .T. ) ;
#99857=DIRECTION ( 'NONE',  ( 1.000000000000000000, 0.000000000000000000, 0.000000000000000000 ) ) ;
#99858=EDGE_CURVE ( 'NONE', #63474, #3210, #5431, .T. ) ;
#99862=DIRECTION ( 'NONE',  ( 0.6830127018922180770, -0.6830127018922204085, -0.2588190451025213501 ) ) ;
#99864=CARTESIAN_POINT ( 'NONE',  ( -16.49999999999987921, -7.912538124160673370, 4.000000000000000000 ) ) ;
#99866=AXIS2_PLACEMENT_3D ( 'NONE', #40717, #5896, #105932 ) ;
#99868=LINE ( 'NONE', #43358, #67494 ) ;
#99869=VECTOR ( 'NONE', #106780, 1000.000000000000227 ) ;
#99870=DIRECTION ( 'NONE',  ( -0.6830127018922180770, -0.6830127018922204085, -0.2588190451025213501 ) ) ;
#99871=VERTEX_POINT ( 'NONE', #114895 ) ;
#99872=VERTEX_POINT ( 'NONE', #6839 ) ;
#99874=VERTEX_POINT ( 'NONE', #51122 ) ;
#99877=DIRECTION ( 'NONE',  ( -0.6830127018922181881, 0.6830127018922202975, -0.2588190451025214056 ) ) ;
#99878=LINE ( 'NONE', #89712, #141217 ) ;
#99879=CARTESIAN_POINT ( 'NONE',  ( -63.29974487139158867, -27.71228299555250274, 4.000000000000000000 ) ) ;
#99880=VECTOR ( 'NONE', #99633, 1000.000000000000000 ) ;
#99882=VERTEX_POINT ( 'NONE', #15573 ) ;
#99885=PLANE ( 'NONE',  #104355 ) ;
#99886=EDGE_CURVE ( 'NONE', #33831, #33645, #61324, .T. ) ;
#99887=DIRECTION ( 'NONE',  ( 0.7071067811865487940, 0.7071067811865463515, 0.000000000000000000 ) ) ;
#99888=CARTESIAN_POINT ( 'NONE',  ( 30.29974487139158867, -27.71228299555227537, 4.000000000000000000 ) ) ;
#99890=FACE_OUTER_BOUND ( 'NONE', #87159, .T. ) ;
#99891=DIRECTION ( 'NONE',  ( -0.7071067811865487940, 0.7071067811865463515, 0.000000000000000000 ) ) ;
#99892=VECTOR ( 'NONE', #91682, 1000.000000000000000 ) ;
#99894=DIRECTION ( 'NONE',  ( -0.6830127018922181881, 0.6830127018922202975, -0.2588190451025214056 ) ) ;
#99895=CARTESIAN_POINT ( 'NONE',  ( 0.000000000000000000, 0.000000000000000000, 5.000000000000000000 ) ) ;
#99896=EDGE_LOOP ( 'NONE', ( #108451, #133012, #59440, #97172 ) ) ;
#99897=ORIENTED_EDGE ( 'NONE', *, *, #96635, .T. ) ;
#99898=EDGE_LOOP ( 'NONE', ( #87238, #97027, #11701, #140940 ) ) ;
#99900=VERTEX_POINT ( 'NONE', #4683 ) ;
#99901=CARTESIAN_POINT ( 'NONE',  ( -1.499999999999980460, -17.94781430457065241, 5.000000000000000000 ) ) ;
#99903=CARTESIAN_POINT ( 'NONE',  ( -25.17183060077628909, -11.24070752338416845, 4.000000000000000000 ) ) ;
#99905=VERTEX_POINT ( 'NONE', #48983 ) ;
#99908=DIRECTION ( 'NONE',  ( -0.7071067811865486830, -0.7071067811865464625, 0.000000000000000000 ) ) ;
#99909=AXIS2_PLACEMENT_3D ( 'NONE', #74865, #95145, #140109 ) ;
#99910=VECTOR ( 'NONE', #75871, 1000.000000000000000 ) ;
#99913=EDGE_CURVE ( 'NONE', #61971, #48649, #93184, .T. ) ;
#99914=PLANE ( 'NONE',  #85977 ) ;
#99915=VECTOR ( 'NONE', #38173, 1000.000000000000000 ) ;
#99916=VECTOR ( 'NONE', #20869, 1000.000000000000000 ) ;
#99918=CIRCLE ( 'NONE', #28096, 5.968999999999998529 ) ;
#99920=ORIENTED_EDGE ( 'NONE', *, *, #7766, .F. ) ;
#99921=ORIENTED_EDGE ( 'NONE', *, *, #118964, .F. ) ;
#99922=EDGE_CURVE ( 'NONE', #74191, #107568, #27926, .T. ) ;
#99923=ORIENTED_EDGE ( 'NONE', *, *, #107056, .F. ) ;
#99924=DIRECTION ( 'NONE',  ( -0.7071067811865486830, 0.7071067811865464625, 0.000000000000000000 ) ) ;
#99925=EDGE_CURVE ( 'NONE', #80487, #131140, #73581, .T. ) ;
#99926=DIRECTION ( 'NONE',  ( 0.6830127018922181881, 0.6830127018922202975, -0.2588190451025214056 ) ) ;
#99928=CARTESIAN_POINT ( 'NONE',  ( 36.48921356237310221, -27.52281430457080802, 5.000000000000000000 ) ) ;
#99929=VECTOR ( 'NONE', #23578, 1000.000000000000000 ) ;
#99931=PLANE ( 'NONE',  #44183 ) ;
#99932=LINE ( 'NONE', #124540, #84457 ) ;
#99933=EDGE_CURVE ( 'NONE', #51489, #134381, #94593, .T. ) ;
#99935=EDGE_CURVE ( 'NONE', #45624, #16581, #126508, .T. ) ;
#99936=EDGE_LOOP ( 'NONE', ( #64051, #74628, #108804, #101872 ) ) ;
#99937=DIRECTION ( 'NONE',  ( -0.3543493200069162685, -0.000000000000000000, -0.9351131265310288487 ) ) ;
#99938=ORIENTED_EDGE ( 'NONE', *, *, #16984, .T. ) ;
#99939=ORIENTED_EDGE ( 'NONE', *, *, #130876, .T. ) ;
#99940=EDGE_CURVE ( 'NONE', #24642, #60272, #106165, .T. ) ;
#99941=AXIS2_PLACEMENT_3D ( 'NONE', #122566, #20390, #99370 ) ;
#99942=AXIS2_PLACEMENT_3D ( 'NONE', #79476, #135257, #37351 ) ;
#99943=LINE ( 'NONE', #107921, #49802 ) ;
#99944=EDGE_LOOP ( 'NONE', ( #30604, #80721, #43691, #66249, #113160, #132400 ) ) ;
#99946=LINE ( 'NONE', #69481, #63414 ) ;
#99947=VECTOR ( 'NONE', #139417, 999.9999999999998863 ) ;
#99948=PLANE ( 'NONE',  #114964 ) ;
#99949=CARTESIAN_POINT ( 'NONE',  ( 51.48921356237309510, -27.52281430457091460, 5.000000000000000000 ) ) ;
#99950=VECTOR ( 'NONE', #37863, 1000.000000000000000 ) ;
#99953=CARTESIAN_POINT ( 'NONE',  ( 11.99999999999992006, -6.033600742197674727, 5.000000000000000000 ) ) ;
#99954=ORIENTED_EDGE ( 'NONE', *, *, #32331, .F. ) ;
#99955=CARTESIAN_POINT ( 'NONE',  ( -27.48921356237309155, -27.52281430457074762, 5.000000000000000000 ) ) ;
#99956=ORIENTED_EDGE ( 'NONE', *, *, #10481, .T. ) ;
#99958=VERTEX_POINT ( 'NONE', #104771 ) ;
#99959=CARTESIAN_POINT ( 'NONE',  ( 19.82816939922340538, 21.75929247661549937, 4.000000000000000000 ) ) ;
#99960=EDGE_LOOP ( 'NONE', ( #141048, #122285, #107988, #13251 ) ) ;
#99961=ORIENTED_EDGE ( 'NONE', *, *, #119403, .T. ) ;
#99962=VECTOR ( 'NONE', #128657, 1000.000000000000000 ) ;
#99963=EDGE_LOOP ( 'NONE', ( #76026, #72925, #10058, #24202, #3002 ) ) ;
#99964=DIRECTION ( 'NONE',  ( 0.7071067811865487940, 0.7071067811865463515, 0.000000000000000000 ) ) ;
#99967=DIRECTION ( 'NONE',  ( 0.7071067811865487940, -0.7071067811865463515, 0.000000000000000000 ) ) ;
#99969=CARTESIAN_POINT ( 'NONE',  ( -36.48921356237310221, -27.52281430457080802, 5.000000000000000000 ) ) ;
#99970=ADVANCED_FACE ( 'NONE', ( #39540 ), #72912, .F. ) ;
#99971=DIRECTION ( 'NONE',  ( -0.6830127018922180770, -0.6830127018922204085, -0.2588190451025213501 ) ) ;
#99972=AXIS2_PLACEMENT_3D ( 'NONE', #108599, #9279, #120936 ) ;
#99973=CARTESIAN_POINT ( 'NONE',  ( 0.000000000000000000, 0.000000000000000000, 5.000000000000000000 ) ) ;
#99974=VECTOR ( 'NONE', #127684, 1000.000000000000000 ) ;
#99975=FACE_OUTER_BOUND ( 'NONE', #51768, .T. ) ;
#99976=EDGE_CURVE ( 'NONE', #142084, #28403, #9725, .T. ) ;
#99977=ADVANCED_FACE ( 'NONE', ( #42403 ), #130839, .F. ) ;
#99979=ORIENTED_EDGE ( 'NONE', *, *, #54793, .F. ) ;
#99980=DIRECTION ( 'NONE',  ( -0.6830127018922181881, 0.6830127018922202975, -0.2588190451025214056 ) ) ;
#99982=VERTEX_POINT ( 'NONE', #141700 ) ;
#99983=ORIENTED_EDGE ( 'NONE', *, *, #112457, .F. ) ;
#99984=ORIENTED_EDGE ( 'NONE', *, *, #72580, .T. ) ;
#99985=AXIS2_PLACEMENT_3D ( 'NONE', #138713, #83632, #27068 ) ;
#99986=DIRECTION ( 'NONE',  ( 0.7071067811865487940, 0.7071067811865463515, 0.000000000000000000 ) ) ;
#99989=EDGE_LOOP ( 'NONE', ( #64506, #50536, #14567, #47655, #86803 ) ) ;
#99990=DIRECTION ( 'NONE',  ( -0.000000000000000000, 0.3543493200069153248, 0.9351131265310292928 ) ) ;
#99991=DIRECTION ( 'NONE',  ( -0.7071067811865487940, 0.7071067811865463515, -0.000000000000000000 ) ) ;
#99992=DIRECTION ( 'NONE',  ( 0.6830127018922180770, -0.6830127018922204085, -0.2588190451025213501 ) ) ;
#99993=EDGE_CURVE ( 'NONE', #71933, #30765, #119896, .T. ) ;
#99994=FACE_OUTER_BOUND ( 'NONE', #29344, .T. ) ;
#99995=EDGE_CURVE ( 'NONE', #91707, #78330, #77179, .T. ) ;
#99996=PLANE ( 'NONE',  #39508 ) ;
#99998=LINE ( 'NONE', #42778, #39472 ) ;
#100000=ORIENTED_EDGE ( 'NONE', *, *, #115359, .T. ) ;
#100003=ORIENTED_EDGE ( 'NONE', *, *, #18077, .T. ) ;
#100006=FACE_OUTER_BOUND ( 'NONE', #19764, .T. ) ;
#100007=LINE ( 'NONE', #44961, #51176 ) ;
#100008=ORIENTED_EDGE ( 'NONE', *, *, #132939, .F. ) ;
#100009=VERTEX_POINT ( 'NONE', #31502 ) ;
#100010=VERTEX_POINT ( 'NONE', #142418 ) ;
#100011=CARTESIAN_POINT ( 'NONE',  ( 39.48921356237310221, -27.52281430457082934, 5.000000000000000000 ) ) ;
#100012=PLANE ( 'NONE',  #74161 ) ;
#100013=DIRECTION ( 'NONE',  ( -0.6830127018922181881, 0.6830127018922202975, -0.2588190451025214056 ) ) ;
#100014=VECTOR ( 'NONE', #41521, 999.9999999999998863 ) ;
#100017=VECTOR ( 'NONE', #111010, 1000.000000000000000 ) ;
#100018=DIRECTION ( 'NONE',  ( 0.7071067811865487940, 0.7071067811865463515, 0.000000000000000000 ) ) ;
#100019=CARTESIAN_POINT ( 'NONE',  ( 54.29974487139159578, -27.71228299555243879, 4.000000000000000000 ) ) ;
#100021=VECTOR ( 'NONE', #115800, 999.9999999999998863 ) ;
#100023=VECTOR ( 'NONE', #32008, 1000.000000000000000 ) ;
#100024=CARTESIAN_POINT ( 'NONE',  ( -20.29289321881331531, -12.74070752338415602, 5.000000000000000000 ) ) ;
#100026=ORIENTED_EDGE ( 'NONE', *, *, #85392, .T. ) ;
#100027=FACE_OUTER_BOUND ( 'NONE', #79156, .T. ) ;
#100028=VECTOR ( 'NONE', #366, 999.9999999999998863 ) ;
#100029=EDGE_CURVE ( 'NONE', #33166, #119697, #109036, .T. ) ;
#100032=AXIS2_PLACEMENT_3D ( 'NONE', #35567, #13736, #79070 ) ;
#100033=DIRECTION ( 'NONE',  ( 0.6830127018922180770, -0.6830127018922204085, -0.2588190451025213501 ) ) ;
#100034=ORIENTED_EDGE ( 'NONE', *, *, #66495, .F. ) ;
#100035=CARTESIAN_POINT ( 'NONE',  ( 7.499999999999951150, -20.56887692260760048, 4.000000000000000000 ) ) ;
#100036=ORIENTED_EDGE ( 'NONE', *, *, #78179, .F. ) ;
#100037=ORIENTED_EDGE ( 'NONE', *, *, #53671, .T. ) ;
#100038=PLANE ( 'NONE',  #102570 ) ;
#100039=DIRECTION ( 'NONE',  ( 0.7071067811865487940, 0.7071067811865463515, -0.000000000000000000 ) ) ;
#100040=VERTEX_POINT ( 'NONE', #132272 ) ;
#100042=CARTESIAN_POINT ( 'NONE',  ( 15.48921356237309510, -27.52281430457066236, 5.000000000000000000 ) ) ;
#100043=ADVANCED_FACE ( 'NONE', ( #32961 ), #140263, .T. ) ;
#100044=CARTESIAN_POINT ( 'NONE',  ( 27.18398860626900060, 28.73617430169806042, 5.000000000000000000 ) ) ;
#100045=DIRECTION ( 'NONE',  ( -0.000000000000000000, 0.000000000000000000, 1.000000000000000000 ) ) ;
#100046=DIRECTION ( 'NONE',  ( 0.7071067811865487940, -0.7071067811865463515, 0.000000000000000000 ) ) ;
#100047=DIRECTION ( 'NONE',  ( 0.7071067811865487940, -0.7071067811865463515, 0.000000000000000000 ) ) ;
#100048=CARTESIAN_POINT ( 'NONE',  ( 7.748455871324196664, -11.24070752338417201, 10.39518518046007145 ) ) ;
#100049=DIRECTION ( 'NONE',  ( -0.7071067811865487940, 0.7071067811865463515, 0.000000000000000000 ) ) ;
#100051=CARTESIAN_POINT ( 'NONE',  ( 39.48921356237310221, -27.52281430457082934, 5.000000000000000000 ) ) ;
#100052=CARTESIAN_POINT ( 'NONE',  ( -13.49999999999991473, 1.030536316426498233, -5.498701923753769094 ) ) ;
#100053=EDGE_CURVE ( 'NONE', #102312, #536, #74302, .T. ) ;
#100054=PLANE ( 'NONE',  #67376 ) ;
#100055=DIRECTION ( 'NONE',  ( -0.000000000000000000, -0.3543493200069152693, 0.9351131265310292928 ) ) ;
#100056=VERTEX_POINT ( 'NONE', #30807 ) ;
#100058=ORIENTED_EDGE ( 'NONE', *, *, #61229, .T. ) ;
#100061=ORIENTED_EDGE ( 'NONE', *, *, #57061, .F. ) ;
#100063=ORIENTED_EDGE ( 'NONE', *, *, #95639, .F. ) ;
#100065=CARTESIAN_POINT ( 'NONE',  ( 23.99999999999983302, 10.55218569542905982, 5.000000000000000000 ) ) ;
#100066=VECTOR ( 'NONE', #93478, 1000.000000000000000 ) ;
#100067=VERTEX_POINT ( 'NONE', #52524 ) ;
#100068=DIRECTION ( 'NONE',  ( 0.3543493200069162685, -0.000000000000000000, -0.9351131265310288487 ) ) ;
#100069=LINE ( 'NONE', #55136, #90462 ) ;
#100070=LINE ( 'NONE', #41385, #132133 ) ;
#100071=DIRECTION ( 'NONE',  ( -0.6830127018922181881, 0.6830127018922202975, -0.2588190451025214056 ) ) ;
#100072=EDGE_LOOP ( 'NONE', ( #81377, #89764, #120379, #133548 ) ) ;
#100073=DIRECTION ( 'NONE',  ( 0.7071067811865487940, 0.7071067811865463515, 0.000000000000000000 ) ) ;
#100074=CARTESIAN_POINT ( 'NONE',  ( 0.000000000000000000, 0.000000000000000000, 5.000000000000000000 ) ) ;
#100075=CARTESIAN_POINT ( 'NONE',  ( 16.17183060077635659, -17.24070752338410628, 4.000000000000000000 ) ) ;
#100077=PLANE ( 'NONE',  #90907 ) ;
#100078=CARTESIAN_POINT ( 'NONE',  ( -45.48921356237309510, -27.52281430457087197, 5.000000000000000000 ) ) ;
#100080=DIRECTION ( 'NONE',  ( 0.7071067811865487940, 0.7071067811865463515, 0.000000000000000000 ) ) ;
#100082=ORIENTED_EDGE ( 'NONE', *, *, #102902, .T. ) ;
#100084=ORIENTED_EDGE ( 'NONE', *, *, #24904, .T. ) ;
#100086=VECTOR ( 'NONE', #43939, 999.9999999999998863 ) ;
#100087=CARTESIAN_POINT ( 'NONE',  ( -34.49999999999976552, 1.030536316426473809, -5.498701923753725573 ) ) ;
#100088=AXIS2_PLACEMENT_3D ( 'NONE', #135537, #60121, #127494 ) ;
#100089=CARTESIAN_POINT ( 'NONE',  ( 26.30673006690384952, -3.740707523384244837, 12.88036043432861533 ) ) ;
#100090=LINE ( 'NONE', #121807, #134665 ) ;
#100093=ORIENTED_EDGE ( 'NONE', *, *, #128438, .T. ) ;
#100094=AXIS2_PLACEMENT_3D ( 'NONE', #76870, #23126, #66684 ) ;
#100095=CARTESIAN_POINT ( 'NONE',  ( 24.79289321881328689, 15.75929247661555976, 5.000000000000000000 ) ) ;
#100096=CARTESIAN_POINT ( 'NONE',  ( -3.005480084712505828, 28.92564299267936079, 4.000000000000000000 ) ) ;
#100098=VERTEX_POINT ( 'NONE', #88756 ) ;
#100100=EDGE_CURVE ( 'NONE', #97786, #78830, #68967, .T. ) ;
#100101=ORIENTED_EDGE ( 'NONE', *, *, #135362, .T. ) ;
#100103=CARTESIAN_POINT ( 'NONE',  ( -19.49999999999986500, 13.56627193232213102, -10.57019076586072970 ) ) ;
#100105=CARTESIAN_POINT ( 'NONE',  ( -6.299744871391586898, -27.71228299555210484, 4.000000000000000000 ) ) ;
#100106=VECTOR ( 'NONE', #47345, 999.9999999999998863 ) ;
#100107=EDGE_CURVE ( 'NONE', #41056, #73002, #58109, .T. ) ;
#100109=ORIENTED_EDGE ( 'NONE', *, *, #50804, .F. ) ;
#100110=ADVANCED_FACE ( 'NONE', ( #37019 ), #92099, .T. ) ;
#100111=LINE ( 'NONE', #87093, #105704 ) ;
#100112=ORIENTED_EDGE ( 'NONE', *, *, #34819, .T. ) ;
#100113=ORIENTED_EDGE ( 'NONE', *, *, #65967, .T. ) ;
#100114=VECTOR ( 'NONE', #73819, 1000.000000000000000 ) ;
#100117=VECTOR ( 'NONE', #140559, 1000.000000000000227 ) ;
#100118=VECTOR ( 'NONE', #111953, 999.9999999999998863 ) ;
#100119=ADVANCED_FACE ( 'NONE', ( #115985 ), #93552, .F. ) ;
#100120=DIRECTION ( 'NONE',  ( -0.7071067811865487940, 0.7071067811865463515, -0.000000000000000000 ) ) ;
#100121=VERTEX_POINT ( 'NONE', #126181 ) ;
#100122=CARTESIAN_POINT ( 'NONE',  ( 51.18398860626899705, 28.73617430169823095, 5.000000000000000000 ) ) ;
#100123=AXIS2_PLACEMENT_3D ( 'NONE', #47362, #121979, #69807 ) ;
#100124=DIRECTION ( 'NONE',  ( -0.000000000000000000, 0.000000000000000000, 1.000000000000000000 ) ) ;
#100127=EDGE_CURVE ( 'NONE', #61837, #89365, #132985, .T. ) ;
#100128=DIRECTION ( 'NONE',  ( -0.3543493200069162685, -0.000000000000000000, -0.9351131265310288487 ) ) ;
#100129=FACE_BOUND ( 'NONE', #59665, .T. ) ;
#100130=ORIENTED_EDGE ( 'NONE', *, *, #59651, .F. ) ;
#100132=DIRECTION ( 'NONE',  ( 1.000000000000000000, 0.000000000000000000, 0.000000000000000000 ) ) ;
#100133=DIRECTION ( 'NONE',  ( 0.7071067811865487940, 0.7071067811865463515, 0.000000000000000000 ) ) ;
#100134=DIRECTION ( 'NONE',  ( -0.7071067811865486830, -0.7071067811865464625, -0.000000000000000000 ) ) ;
#100135=ORIENTED_EDGE ( 'NONE', *, *, #111734, .T. ) ;
#100136=DIRECTION ( 'NONE',  ( -0.7071067811865486830, -0.7071067811865464625, 0.000000000000000000 ) ) ;
#100137=ORIENTED_EDGE ( 'NONE', *, *, #20728, .F. ) ;
#100138=ADVANCED_FACE ( 'NONE', ( #33664 ), #80552, .F. ) ;
#100139=ORIENTED_EDGE ( 'NONE', *, *, #21378, .T. ) ;
#100140=EDGE_CURVE ( 'NONE', #58586, #58453, #71819, .T. ) ;
#100141=ORIENTED_EDGE ( 'NONE', *, *, #102990, .T. ) ;
#100143=VERTEX_POINT ( 'NONE', #114568 ) ;
#100144=VECTOR ( 'NONE', #95163, 1000.000000000000000 ) ;
#100145=PLANE ( 'NONE',  #62604 ) ;
#100146=DIRECTION ( 'NONE',  ( 0.6830127018922181881, 0.6830127018922202975, -0.2588190451025214056 ) ) ;
#100147=EDGE_CURVE ( 'NONE', #58174, #81446, #26854, .T. ) ;
#100148=ORIENTED_EDGE ( 'NONE', *, *, #3995, .F. ) ;
#100149=DIRECTION ( 'NONE',  ( 0.7071067811865487940, 0.7071067811865463515, 0.000000000000000000 ) ) ;
#100150=FACE_OUTER_BOUND ( 'NONE', #49549, .T. ) ;
#100151=VECTOR ( 'NONE', #41293, 1000.000000000000000 ) ;
#100152=EDGE_CURVE ( 'NONE', #55245, #79341, #16691, .T. ) ;
#100153=EDGE_CURVE ( 'NONE', #119622, #38956, #115245, .T. ) ;
#100154=DIRECTION ( 'NONE',  ( 0.7071067811865486830, -0.7071067811865464625, -0.000000000000000000 ) ) ;
#100155=PLANE ( 'NONE',  #115647 ) ;
#100157=VECTOR ( 'NONE', #10635, 1000.000000000000000 ) ;
#100158=PLANE ( 'NONE',  #63311 ) ;
#100160=VERTEX_POINT ( 'NONE', #137783 ) ;
#100161=ORIENTED_EDGE ( 'NONE', *, *, #110082, .F. ) ;
#100162=ORIENTED_EDGE ( 'NONE', *, *, #143524, .T. ) ;
#100163=EDGE_LOOP ( 'NONE', ( #72644, #25334, #79076, #66990 ) ) ;
#100164=VECTOR ( 'NONE', #76923, 1000.000000000000000 ) ;
#100165=FACE_OUTER_BOUND ( 'NONE', #31035, .T. ) ;
#100168=EDGE_CURVE ( 'NONE', #59322, #100356, #83394, .T. ) ;
#100169=VERTEX_POINT ( 'NONE', #95677 ) ;
#100171=PLANE ( 'NONE',  #101205 ) ;
#100172=ADVANCED_FACE ( 'NONE', ( #97061 ), #73937, .F. ) ;
#100173=CARTESIAN_POINT ( 'NONE',  ( -17.99999999999986144, 20.58746187583903620, 4.000000000000000000 ) ) ;
#100174=ORIENTED_EDGE ( 'NONE', *, *, #28660, .T. ) ;
#100175=FACE_OUTER_BOUND ( 'NONE', #14414, .T. ) ;
#100176=DIRECTION ( 'NONE',  ( -0.7071067811865486830, -0.7071067811865464625, 0.000000000000000000 ) ) ;
#100178=DIRECTION ( 'NONE',  ( -0.000000000000000000, -0.3543493200069152693, 0.9351131265310292928 ) ) ;
#100179=VERTEX_POINT ( 'NONE', #130478 ) ;
#100181=EDGE_CURVE ( 'NONE', #74923, #36339, #31164, .T. ) ;
#100182=LINE ( 'NONE', #63980, #104457 ) ;
#100183=AXIS2_PLACEMENT_3D ( 'NONE', #100495, #3288, #59160 ) ;
#100184=LINE ( 'NONE', #34934, #51946 ) ;
#100185=DIRECTION ( 'NONE',  ( 0.7071067811865487940, -0.7071067811865463515, 0.000000000000000000 ) ) ;
#100186=ORIENTED_EDGE ( 'NONE', *, *, #31862, .T. ) ;
#100187=CARTESIAN_POINT ( 'NONE',  ( 39.48921356237310221, -27.52281430457082934, 5.000000000000000000 ) ) ;
#100188=VECTOR ( 'NONE', #3379, 1000.000000000000000 ) ;
#100189=EDGE_LOOP ( 'NONE', ( #125410, #74629, #119173, #44777 ) ) ;
#100190=CARTESIAN_POINT ( 'NONE',  ( -24.48921356237309510, -27.52281430457072631, 5.000000000000000000 ) ) ;
#100191=EDGE_CURVE ( 'NONE', #40356, #123762, #107264, .T. ) ;
#100192=CARTESIAN_POINT ( 'NONE',  ( 2.207106781186533251, 18.75929247661552424, 5.000000000000000000 ) ) ;
#100193=DIRECTION ( 'NONE',  ( -0.000000000000000000, 0.3543493200069153248, 0.9351131265310292928 ) ) ;
#100194=ORIENTED_EDGE ( 'NONE', *, *, #62605, .T. ) ;
#100195=CARTESIAN_POINT ( 'NONE',  ( 26.68342038867194432, -6.740707523384216415, 11.88629033278118108 ) ) ;
#100196=DIRECTION ( 'NONE',  ( -0.000000000000000000, -0.3543493200069152693, 0.9351131265310292928 ) ) ;
#100197=DIRECTION ( 'NONE',  ( -0.000000000000000000, -0.000000000000000000, 1.000000000000000000 ) ) ;
#100198=ORIENTED_EDGE ( 'NONE', *, *, #40086, .T. ) ;
#100199=VECTOR ( 'NONE', #54304, 1000.000000000000227 ) ;
#100200=LINE ( 'NONE', #847, #77058 ) ;
#100201=ORIENTED_EDGE ( 'NONE', *, *, #77580, .F. ) ;
#100203=CYLINDRICAL_SURFACE ( 'NONE', #143473, 0.5000000000000004441 ) ;
#100205=ORIENTED_EDGE ( 'NONE', *, *, #107001, .F. ) ;
#100208=DIRECTION ( 'NONE',  ( -4.681814790819591790E-17, -0.3543493200069152693, 0.9351131265310292928 ) ) ;
#100209=ORIENTED_EDGE ( 'NONE', *, *, #124152, .F. ) ;
#100210=DIRECTION ( 'NONE',  ( 0.3543493200069162685, -0.000000000000000000, -0.9351131265310288487 ) ) ;
#100211=CARTESIAN_POINT ( 'NONE',  ( -17.33153258840132338, -18.74070752338409207, 20.73178291233837101 ) ) ;
#100212=CARTESIAN_POINT ( 'NONE',  ( -29.99999999999978684, 4.931123077392138399, 4.000000000000000000 ) ) ;
#100214=CARTESIAN_POINT ( 'NONE',  ( 14.99999999999989519, -13.39766691384881803, -10.96608748226469210 ) ) ;
#100216=DIRECTION ( 'NONE',  ( -0.7071067811865487940, 0.7071067811865463515, 0.000000000000000000 ) ) ;
#100217=VECTOR ( 'NONE', #26906, 1000.000000000000000 ) ;
#100220=AXIS2_PLACEMENT_3D ( 'NONE', #137821, #70459, #15270 ) ;
#100222=VERTEX_POINT ( 'NONE', #8624 ) ;
#100223=ORIENTED_EDGE ( 'NONE', *, *, #2686, .T. ) ;
#100224=VERTEX_POINT ( 'NONE', #7939 ) ;
#100225=VERTEX_POINT ( 'NONE', #85498 ) ;
#100226=VECTOR ( 'NONE', #56162, 1000.000000000000227 ) ;
#100227=VECTOR ( 'NONE', #17159, 1000.000000000000000 ) ;
#100228=CARTESIAN_POINT ( 'NONE',  ( -39.18398860626899705, 28.73617430169814568, 5.000000000000000000 ) ) ;
#100229=LINE ( 'NONE', #102389, #108696 ) ;
#100230=ORIENTED_EDGE ( 'NONE', *, *, #83308, .F. ) ;
#100231=CARTESIAN_POINT ( 'NONE',  ( 26.99451991528749417, 28.92564299267956685, 4.000000000000000000 ) ) ;
#100232=LINE ( 'NONE', #23361, #92982 ) ;
#100233=DIRECTION ( 'NONE',  ( 0.7071067811865487940, -0.7071067811865463515, 0.000000000000000000 ) ) ;
#100234=FACE_OUTER_BOUND ( 'NONE', #70603, .T. ) ;
#100236=ORIENTED_EDGE ( 'NONE', *, *, #129485, .F. ) ;
#100238=CARTESIAN_POINT ( 'NONE',  ( 13.99806943317892127, -22.22500000000000142, 4.500000000000000888 ) ) ;
#100239=DIRECTION ( 'NONE',  ( 0.7071067811865486830, -0.7071067811865464625, -0.000000000000000000 ) ) ;
#100241=CARTESIAN_POINT ( 'NONE',  ( 24.48921356237309510, -27.52281430457072631, 5.000000000000000000 ) ) ;
#100242=DIRECTION ( 'NONE',  ( -0.7071067811865487940, 0.7071067811865463515, 0.000000000000000000 ) ) ;
#100243=LINE ( 'NONE', #97345, #45828 ) ;
#100245=PLANE ( 'NONE',  #69988 ) ;
#100246=VECTOR ( 'NONE', #44620, 1000.000000000000000 ) ;
#100247=PLANE ( 'NONE',  #50803 ) ;
#100248=ORIENTED_EDGE ( 'NONE', *, *, #142835, .F. ) ;
#100249=ORIENTED_EDGE ( 'NONE', *, *, #5155, .T. ) ;
#100251=CARTESIAN_POINT ( 'NONE',  ( -45.48921356237309510, -27.52281430457087197, 5.000000000000000000 ) ) ;
#100252=ADVANCED_FACE ( 'NONE', ( #75374 ), #63793, .F. ) ;
#100253=LINE ( 'NONE', #133605, #108595 ) ;
#100254=ORIENTED_EDGE ( 'NONE', *, *, #126878, .T. ) ;
#100255=LINE ( 'NONE', #132183, #52539 ) ;
#100256=AXIS2_PLACEMENT_3D ( 'NONE', #29525, #30253, #96900 ) ;
#100257=DIRECTION ( 'NONE',  ( -0.7071067811865486830, -0.7071067811865464625, 0.000000000000000000 ) ) ;
#100259=VECTOR ( 'NONE', #59051, 1000.000000000000227 ) ;
#100260=ORIENTED_EDGE ( 'NONE', *, *, #112708, .T. ) ;
#100262=ORIENTED_EDGE ( 'NONE', *, *, #97993, .T. ) ;
#100263=EDGE_LOOP ( 'NONE', ( #107970, #33967, #111180, #105870 ) ) ;
#100265=DIRECTION ( 'NONE',  ( 0.7071067811865487940, 0.7071067811865463515, -0.000000000000000000 ) ) ;
#100266=DIRECTION ( 'NONE',  ( -0.000000000000000000, 0.3543493200069152138, -0.9351131265310292928 ) ) ;
#100267=EDGE_CURVE ( 'NONE', #3922, #76836, #30437, .T. ) ;
#100268=CARTESIAN_POINT ( 'NONE',  ( -34.92500000000001137, -22.22500000000000142, 0.4999999999999995559 ) ) ;
#100269=ORIENTED_EDGE ( 'NONE', *, *, #86501, .F. ) ;
#100270=DIRECTION ( 'NONE',  ( 0.000000000000000000, -1.000000000000000000, 0.000000000000000000 ) ) ;
#100271=EDGE_CURVE ( 'NONE', #31963, #94490, #7211, .T. ) ;
#100272=EDGE_CURVE ( 'NONE', #80339, #5588, #105819, .T. ) ;
#100273=ORIENTED_EDGE ( 'NONE', *, *, #76639, .F. ) ;
#100274=LINE ( 'NONE', #46657, #30906 ) ;
#100276=PLANE ( 'NONE',  #22295 ) ;
#100278=CARTESIAN_POINT ( 'NONE',  ( -4.828169399223498637, 6.759292476615651246, 4.000000000000000000 ) ) ;
#100280=AXIS2_PLACEMENT_3D ( 'NONE', #102889, #26040, #137667 ) ;
#100281=EDGE_CURVE ( 'NONE', #16142, #15535, #51484, .T. ) ;
#100282=EDGE_CURVE ( 'NONE', #42749, #22851, #117408, .T. ) ;
#100284=VECTOR ( 'NONE', #77913, 1000.000000000000000 ) ;
#100288=ADVANCED_FACE ( 'NONE', ( #139932 ), #40609, .F. ) ;
#100289=VECTOR ( 'NONE', #17722, 1000.000000000000000 ) ;
#100291=CARTESIAN_POINT ( 'NONE',  ( 0.000000000000000000, 0.000000000000000000, 5.000000000000000000 ) ) ;
#100292=ORIENTED_EDGE ( 'NONE', *, *, #53462, .F. ) ;
#100294=LINE ( 'NONE', #78539, #37696 ) ;
#100295=ORIENTED_EDGE ( 'NONE', *, *, #110295, .T. ) ;
#100296=EDGE_CURVE ( 'NONE', #101043, #111265, #28300, .T. ) ;
#100297=CARTESIAN_POINT ( 'NONE',  ( 20.99999999999986855, 17.58746187583907172, 4.000000000000000000 ) ) ;
#100298=ORIENTED_EDGE ( 'NONE', *, *, #106570, .T. ) ;
#100299=DIRECTION ( 'NONE',  ( 0.7071067811865487940, 0.7071067811865463515, 0.000000000000000000 ) ) ;
#100300=PLANE ( 'NONE',  #31749 ) ;
#100301=LINE ( 'NONE', #123506, #2179 ) ;
#100302=VECTOR ( 'NONE', #25482, 1000.000000000000000 ) ;
#100304=FACE_BOUND ( 'NONE', #74689, .T. ) ;
#100305=DIRECTION ( 'NONE',  ( 0.3543493200069162685, -0.000000000000000000, -0.9351131265310288487 ) ) ;
#100306=DIRECTION ( 'NONE',  ( 0.7071067811865487940, -0.7071067811865463515, 0.000000000000000000 ) ) ;
#100307=VECTOR ( 'NONE', #61272, 1000.000000000000000 ) ;
#100308=DIRECTION ( 'NONE',  ( 0.6830127018922180770, -0.6830127018922204085, -0.2588190451025213501 ) ) ;
#100309=DIRECTION ( 'NONE',  ( -0.000000000000000000, -0.3543493200069152693, 0.9351131265310292928 ) ) ;
#100310=ORIENTED_EDGE ( 'NONE', *, *, #84447, .F. ) ;
#100311=EDGE_CURVE ( 'NONE', #43879, #22057, #129732, .T. ) ;
#100313=EDGE_LOOP ( 'NONE', ( #2205, #27237, #14532, #15640 ) ) ;
#100314=ORIENTED_EDGE ( 'NONE', *, *, #82799, .T. ) ;
#100316=ORIENTED_EDGE ( 'NONE', *, *, #5223, .T. ) ;
#100317=CARTESIAN_POINT ( 'NONE',  ( 47.99451991528749062, 28.92564299267971251, 4.000000000000000000 ) ) ;
#100318=EDGE_CURVE ( 'NONE', #46180, #4087, #127612, .T. ) ;
#100319=EDGE_LOOP ( 'NONE', ( #97499, #93307, #57086, #17318 ) ) ;
#100320=DIRECTION ( 'NONE',  ( -0.6830127018922180770, -0.6830127018922204085, -0.2588190451025213501 ) ) ;
#100321=AXIS2_PLACEMENT_3D ( 'NONE', #15117, #123224, #23893 ) ;
#100323=DIRECTION ( 'NONE',  ( -0.7071067811865486830, 0.7071067811865464625, 0.000000000000000000 ) ) ;
#100324=ADVANCED_FACE ( 'NONE', ( #5788 ), #19547, .F. ) ;
#100325=CARTESIAN_POINT ( 'NONE',  ( 54.29974487139159578, -27.71228299555243879, 4.000000000000000000 ) ) ;
#100326=FACE_OUTER_BOUND ( 'NONE', #50216, .T. ) ;
#100327=DIRECTION ( 'NONE',  ( -0.7071067811865486830, -0.7071067811865464625, 0.000000000000000000 ) ) ;
#100328=EDGE_CURVE ( 'NONE', #24144, #94048, #116724, .T. ) ;
#100331=ORIENTED_EDGE ( 'NONE', *, *, #129468, .F. ) ;
#100332=AXIS2_PLACEMENT_3D ( 'NONE', #118256, #53002, #66067 ) ;
#100333=VERTEX_POINT ( 'NONE', #6480 ) ;
#100334=FACE_OUTER_BOUND ( 'NONE', #45652, .T. ) ;
#100335=DIRECTION ( 'NONE',  ( 0.7071067811865487940, 0.7071067811865463515, -0.000000000000000000 ) ) ;
#100336=VERTEX_POINT ( 'NONE', #139219 ) ;
#100337=ADVANCED_FACE ( 'NONE', ( #99975 ), #67362, .T. ) ;
#100338=ORIENTED_EDGE ( 'NONE', *, *, #85433, .T. ) ;
#100341=ORIENTED_EDGE ( 'NONE', *, *, #21727, .F. ) ;
#100342=CARTESIAN_POINT ( 'NONE',  ( 30.48921356237309510, -27.52281430457076894, 5.000000000000000000 ) ) ;
#100343=VECTOR ( 'NONE', #7386, 1000.000000000000000 ) ;
#100344=EDGE_CURVE ( 'NONE', #57042, #84048, #89112, .T. ) ;
#100345=DIRECTION ( 'NONE',  ( 0.7071067811865486830, -0.7071067811865464625, -0.000000000000000000 ) ) ;
#100346=VECTOR ( 'NONE', #16763, 1000.000000000000000 ) ;
#100349=ORIENTED_EDGE ( 'NONE', *, *, #1110, .F. ) ;
#100350=EDGE_CURVE ( 'NONE', #47692, #74087, #89797, .T. ) ;
#100352=DIRECTION ( 'NONE',  ( -0.6830127018922181881, 0.6830127018922202975, -0.2588190451025214056 ) ) ;
#100353=CARTESIAN_POINT ( 'NONE',  ( -30.32816939922332011, -18.74070752338409562, 4.000000000000000000 ) ) ;
#100354=FACE_OUTER_BOUND ( 'NONE', #101589, .T. ) ;
#100355=EDGE_LOOP ( 'NONE', ( #133381, #47262, #29451, #59398 ) ) ;
#100356=VERTEX_POINT ( 'NONE', #56520 ) ;
#100357=PLANE ( 'NONE',  #3282 ) ;
#100359=VECTOR ( 'NONE', #40286, 1000.000000000000000 ) ;
#100360=DIRECTION ( 'NONE',  ( -1.000000000000000000, 0.000000000000000000, 0.000000000000000000 ) ) ;
#100361=ORIENTED_EDGE ( 'NONE', *, *, #129635, .T. ) ;
#100363=CARTESIAN_POINT ( 'NONE',  ( 33.18398860626899705, 28.73617430169810305, 5.000000000000000000 ) ) ;
#100364=VERTEX_POINT ( 'NONE', #120996 ) ;
#100365=ADVANCED_FACE ( 'NONE', ( #134039 ), #87667, .F. ) ;
#100366=VECTOR ( 'NONE', #87341, 1000.000000000000000 ) ;
#100367=DIRECTION ( 'NONE',  ( 0.7071067811865487940, 0.7071067811865463515, 0.000000000000000000 ) ) ;
#100369=CARTESIAN_POINT ( 'NONE',  ( 11.67183060077639567, 5.259292476615665457, 4.000000000000000000 ) ) ;
#100371=CARTESIAN_POINT ( 'NONE',  ( 6.005480084712508493, 28.92564299267933947, 4.000000000000000000 ) ) ;
#100373=VECTOR ( 'NONE', #20641, 1000.000000000000000 ) ;
#100374=LINE ( 'NONE', #25647, #40171 ) ;
#100375=EDGE_CURVE ( 'NONE', #37842, #126541, #43452, .T. ) ;
#100376=CARTESIAN_POINT ( 'NONE',  ( 6.183988606268994381, 28.73617430169791476, 5.000000000000000000 ) ) ;
#100377=ORIENTED_EDGE ( 'NONE', *, *, #72378, .F. ) ;
#100378=ORIENTED_EDGE ( 'NONE', *, *, #16557, .F. ) ;
#100380=DIRECTION ( 'NONE',  ( -0.7071067811865487940, 0.7071067811865463515, -0.000000000000000000 ) ) ;
#100383=FACE_OUTER_BOUND ( 'NONE', #38726, .T. ) ;
#100385=VECTOR ( 'NONE', #119244, 1000.000000000000000 ) ;
#100386=ORIENTED_EDGE ( 'NONE', *, *, #78306, .T. ) ;
#100387=PLANE ( 'NONE',  #15947 ) ;
#100388=PLANE ( 'NONE',  #51093 ) ;
#100389=CARTESIAN_POINT ( 'NONE',  ( 13.10966639810773948, 3.759292476615678336, 4.164048746910661514 ) ) ;
#100391=CARTESIAN_POINT ( 'NONE',  ( 12.70710678118646086, -0.7407075233842770334, 5.000000000000000000 ) ) ;
#100392=LINE ( 'NONE', #109826, #9434 ) ;
#100394=AXIS2_PLACEMENT_3D ( 'NONE', #22751, #35128, #47457 ) ;
#100395=DIRECTION ( 'NONE',  ( -0.6830127018922180770, -0.6830127018922204085, -0.2588190451025213501 ) ) ;
#100397=( BOUNDED_CURVE ( )  B_SPLINE_CURVE ( 3, ( #133191, #136014, #45476, #59215 ),
 .UNSPECIFIED., .F., .F. ) 
 B_SPLINE_CURVE_WITH_KNOTS ( ( 4, 4 ),
 ( 5.043186909253414285, 5.074607125596365620 ),
 .UNSPECIFIED. ) 
 CURVE ( )  GEOMETRIC_REPRESENTATION_ITEM ( )  RATIONAL_B_SPLINE_CURVE ( ( 1.000000000000000000, 0.9999177325257868620, 0.9999177325257868620, 1.000000000000000000 ) ) 
 REPRESENTATION_ITEM ( '' )  );
#100398=EDGE_CURVE ( 'NONE', #38295, #133583, #34018, .T. ) ;
#100399=DIRECTION ( 'NONE',  ( 0.6830127018922181881, 0.6830127018922202975, -0.2588190451025214056 ) ) ;
#100400=CARTESIAN_POINT ( 'NONE',  ( -31.49999999999977263, 0.05218569542916537407, 5.000000000000000000 ) ) ;
#100401=EDGE_CURVE ( 'NONE', #86941, #21557, #132615, .T. ) ;
#100402=DIRECTION ( 'NONE',  ( 0.7071067811865486830, -0.7071067811865464625, -0.000000000000000000 ) ) ;
#100403=VERTEX_POINT ( 'NONE', #120247 ) ;
#100404=ORIENTED_EDGE ( 'NONE', *, *, #132894, .T. ) ;
#100406=CARTESIAN_POINT ( 'NONE',  ( 11.67183060077638856, -12.74070752338415247, 4.000000000000000000 ) ) ;
#100407=LINE ( 'NONE', #1050, #41477 ) ;
#100408=LINE ( 'NONE', #79412, #122998 ) ;
#100409=CARTESIAN_POINT ( 'NONE',  ( -17.99999999999987210, -6.033600742197671174, 5.000000000000000000 ) ) ;
#100412=LINE ( 'NONE', #122132, #89377 ) ;
#100413=ORIENTED_EDGE ( 'NONE', *, *, #14516, .T. ) ;
#100419=LINE ( 'NONE', #43899, #108397 ) ;
#100422=VECTOR ( 'NONE', #17235, 1000.000000000000000 ) ;
#100423=FACE_OUTER_BOUND ( 'NONE', #110415, .T. ) ;
#100424=ORIENTED_EDGE ( 'NONE', *, *, #132591, .T. ) ;
#100426=DIRECTION ( 'NONE',  ( -0.000000000000000000, -0.3543493200069152693, 0.9351131265310292928 ) ) ;
#100427=DIRECTION ( 'NONE',  ( -0.6830127018922181881, 0.6830127018922202975, -0.2588190451025214056 ) ) ;
#100428=DIRECTION ( 'NONE',  ( 0.6830127018922180770, -0.6830127018922204085, -0.2588190451025213501 ) ) ;
#100429=VERTEX_POINT ( 'NONE', #21697 ) ;
#100430=VECTOR ( 'NONE', #67369, 1000.000000000000000 ) ;
#100431=CARTESIAN_POINT ( 'NONE',  ( 10.63753812416090483, 22.22500000000000142, 4.000000000000000000 ) ) ;
#100433=ORIENTED_EDGE ( 'NONE', *, *, #93674, .T. ) ;
#100434=EDGE_CURVE ( 'NONE', #35824, #46067, #20965, .T. ) ;
#100435=ORIENTED_EDGE ( 'NONE', *, *, #84945, .F. ) ;
#100436=LINE ( 'NONE', #4430, #111448 ) ;
#100437=CARTESIAN_POINT ( 'NONE',  ( -32.99999999999977263, -0.8619312979532278707, -5.102805207349900840 ) ) ;
#100439=DIRECTION ( 'NONE',  ( -0.3543493200069162685, -0.000000000000000000, -0.9351131265310288487 ) ) ;
#100441=DIRECTION ( 'NONE',  ( -0.7071067811865486830, -0.7071067811865464625, 0.000000000000000000 ) ) ;
#100442=ORIENTED_EDGE ( 'NONE', *, *, #133595, .T. ) ;
#100443=CARTESIAN_POINT ( 'NONE',  ( -0.7071067811865381358, -6.740707523384216415, 5.000000000000000000 ) ) ;
#100444=PLANE ( 'NONE',  #131006 ) ;
#100445=CARTESIAN_POINT ( 'NONE',  ( 0.000000000000000000, 21.72500000000000142, 4.500000000000000888 ) ) ;
#100446=CARTESIAN_POINT ( 'NONE',  ( -34.42500000000001137, 21.72500000000000142, 0.4999999999999995559 ) ) ;
#100447=ORIENTED_EDGE ( 'NONE', *, *, #60923, .F. ) ;
#100448=EDGE_CURVE ( 'NONE', #48047, #125864, #34725, .T. ) ;
#100449=EDGE_CURVE ( 'NONE', #58745, #64560, #99224, .T. ) ;
#100450=ORIENTED_EDGE ( 'NONE', *, *, #57006, .F. ) ;
#100451=EDGE_CURVE ( 'NONE', #40957, #96751, #68671, .T. ) ;
#100454=ORIENTED_EDGE ( 'NONE', *, *, #124363, .T. ) ;
#100455=EDGE_CURVE ( 'NONE', #64729, #5522, #64486, .T. ) ;
#100457=LINE ( 'NONE', #78699, #54992 ) ;
#100458=EDGE_CURVE ( 'NONE', #21974, #94538, #33333, .T. ) ;
#100459=DIRECTION ( 'NONE',  ( 0.6830127018922181881, 0.6830127018922202975, -0.2588190451025214056 ) ) ;
#100460=LINE ( 'NONE', #11994, #57133 ) ;
#100461=VERTEX_POINT ( 'NONE', #10096 ) ;
#100462=ORIENTED_EDGE ( 'NONE', *, *, #52827, .F. ) ;
#100463=ADVANCED_FACE ( 'NONE', ( #55773 ), #637, .F. ) ;
#100464=FACE_OUTER_BOUND ( 'NONE', #114344, .T. ) ;
#100467=ADVANCED_FACE ( 'NONE', ( #126020 ), #91266, .F. ) ;
#100468=ORIENTED_EDGE ( 'NONE', *, *, #134840, .T. ) ;
#100469=AXIS2_PLACEMENT_3D ( 'NONE', #120288, #19585, #41327 ) ;
#100471=AXIS2_PLACEMENT_3D ( 'NONE', #108963, #9658, #53930 ) ;
#100472=DIRECTION ( 'NONE',  ( 0.6830127018922180770, -0.6830127018922204085, -0.2588190451025213501 ) ) ;
#100473=FACE_OUTER_BOUND ( 'NONE', #139882, .T. ) ;
#100474=VERTEX_POINT ( 'NONE', #48444 ) ;
#100475=VECTOR ( 'NONE', #51715, 999.9999999999998863 ) ;
#100476=EDGE_CURVE ( 'NONE', #69514, #5966, #2788, .T. ) ;
#100477=VECTOR ( 'NONE', #97272, 1000.000000000000000 ) ;
#100478=FACE_BOUND ( 'NONE', #71852, .T. ) ;
#100479=CARTESIAN_POINT ( 'NONE',  ( -10.82816939922345334, 3.759292476615676559, 4.000000000000000000 ) ) ;
#100480=CARTESIAN_POINT ( 'NONE',  ( 34.92499999999998295, 21.72500000000000142, 4.165035510187005130 ) ) ;
#100482=FACE_OUTER_BOUND ( 'NONE', #99898, .T. ) ;
#100483=ADVANCED_FACE ( 'NONE', ( #36158 ), #104218, .F. ) ;
#100484=AXIS2_PLACEMENT_3D ( 'NONE', #66634, #76074, #22368 ) ;
#100485=DIRECTION ( 'NONE',  ( -0.7071067811865487940, 0.7071067811865463515, -0.000000000000000000 ) ) ;
#100487=EDGE_LOOP ( 'NONE', ( #86593, #50574, #28798, #68313 ) ) ;
#100488=VECTOR ( 'NONE', #4160, 1000.000000000000000 ) ;
#100489=ORIENTED_EDGE ( 'NONE', *, *, #13089, .T. ) ;
#100492=PLANE ( 'NONE',  #16499 ) ;
#100493=ORIENTED_EDGE ( 'NONE', *, *, #9965, .T. ) ;
#100494=VECTOR ( 'NONE', #139659, 1000.000000000000000 ) ;
#100495=CARTESIAN_POINT ( 'NONE',  ( -14.81601139373099585, 28.73617430169776910, 5.000000000000000000 ) ) ;
#100497=DIRECTION ( 'NONE',  ( 0.6830127018922181881, 0.6830127018922202975, -0.2588190451025214056 ) ) ;
#100498=ORIENTED_EDGE ( 'NONE', *, *, #83296, .T. ) ;
#100499=CARTESIAN_POINT ( 'NONE',  ( 29.67183060077626067, -9.740707523384182664, 4.000000000000000000 ) ) ;
#100500=LINE ( 'NONE', #78042, #1465 ) ;
#100501=LINE ( 'NONE', #135969, #73539 ) ;
#100502=DIRECTION ( 'NONE',  ( -0.7071067811865487940, 0.7071067811865463515, 0.000000000000000000 ) ) ;
#100504=LINE ( 'NONE', #130995, #46256 ) ;
#100506=CARTESIAN_POINT ( 'NONE',  ( -7.499999999999951150, 11.52377502935401843, -1.522421517564068294 ) ) ;
#100507=ORIENTED_EDGE ( 'NONE', *, *, #94727, .T. ) ;
#100509=EDGE_CURVE ( 'NONE', #76331, #99958, #124579, .T. ) ;
#100510=DIRECTION ( 'NONE',  ( 0.6830127018922180770, -0.6830127018922204085, -0.2588190451025214056 ) ) ;
#100511=ORIENTED_EDGE ( 'NONE', *, *, #97822, .T. ) ;
#100512=ORIENTED_EDGE ( 'NONE', *, *, #39360, .F. ) ;
#100513=ORIENTED_EDGE ( 'NONE', *, *, #109373, .T. ) ;
#100516=ADVANCED_FACE ( 'NONE', ( #91939 ), #26694, .T. ) ;
#100518=AXIS2_PLACEMENT_3D ( 'NONE', #1691, #44573, #22043 ) ;
#100521=DIRECTION ( 'NONE',  ( -0.3543493200069162685, -0.000000000000000000, -0.9351131265310288487 ) ) ;
#100522=EDGE_LOOP ( 'NONE', ( #112186, #93712, #100058, #43892 ) ) ;
#100524=VERTEX_POINT ( 'NONE', #70250 ) ;
#100525=CARTESIAN_POINT ( 'NONE',  ( -4.499999999999974243, 6.431123077392122411, 4.000000000000000000 ) ) ;
#100526=CARTESIAN_POINT ( 'NONE',  ( 24.98480450340313652, 2.536990198832462351, 5.000000000000000000 ) ) ;
#100527=ORIENTED_EDGE ( 'NONE', *, *, #26036, .T. ) ;
#100528=AXIS2_PLACEMENT_3D ( 'NONE', #121506, #101190, #137230 ) ;
#100529=CARTESIAN_POINT ( 'NONE',  ( -22.49999999999984013, -16.53360074219757081, 5.000000000000000000 ) ) ;
#100530=CARTESIAN_POINT ( 'NONE',  ( 75.29974487139158157, -27.71228299555258445, 4.000000000000000000 ) ) ;
#100531=ORIENTED_EDGE ( 'NONE', *, *, #81776, .T. ) ;
#100533=EDGE_CURVE ( 'NONE', #11291, #118868, #114410, .T. ) ;
#100534=ORIENTED_EDGE ( 'NONE', *, *, #67389, .F. ) ;
#100535=ORIENTED_EDGE ( 'NONE', *, *, #24735, .F. ) ;
#100536=VERTEX_POINT ( 'NONE', #70936 ) ;
#100538=PLANE ( 'NONE',  #109359 ) ;
#100540=LINE ( 'NONE', #36687, #2285 ) ;
#100542=ORIENTED_EDGE ( 'NONE', *, *, #51948, .F. ) ;
#100543=AXIS2_PLACEMENT_3D ( 'NONE', #112789, #33828, #91072 ) ;
#100544=CARTESIAN_POINT ( 'NONE',  ( 42.29974487139158157, -27.71228299555235708, 4.000000000000000000 ) ) ;
#100545=VECTOR ( 'NONE', #65499, 1000.000000000000000 ) ;
#100547=ADVANCED_FACE ( 'NONE', ( #123172 ), #38291, .F. ) ;
#100548=CARTESIAN_POINT ( 'NONE',  ( 10.49999999999993605, -14.94781430457067195, 5.000000000000000000 ) ) ;
#100549=CARTESIAN_POINT ( 'NONE',  ( 8.700255128608413102, -27.71228299555199825, 4.000000000000000000 ) ) ;
#100550=ADVANCED_FACE ( 'NONE', ( #93376 ), #36845, .F. ) ;
#100551=( BOUNDED_CURVE ( )  B_SPLINE_CURVE ( 3, ( #120795, #119350, #108454, #120049 ),
 .UNSPECIFIED., .F., .T. ) 
 B_SPLINE_CURVE_WITH_KNOTS ( ( 4, 4 ),
 ( 3.581556339957213897, 3.677360298529522176 ),
 .UNSPECIFIED. ) 
 CURVE ( )  GEOMETRIC_REPRESENTATION_ITEM ( )  RATIONAL_B_SPLINE_CURVE ( ( 1.000000000000000000, 0.9992352797041761381, 0.9992352797041761381, 1.000000000000000000 ) ) 
 REPRESENTATION_ITEM ( '' )  );
#100552=DIRECTION ( 'NONE',  ( 0.7071067811865487940, 0.7071067811865463515, 0.000000000000000000 ) ) ;
#100553=EDGE_LOOP ( 'NONE', ( #94010, #33835, #136661, #44520 ) ) ;
#100554=VECTOR ( 'NONE', #141044, 1000.000000000000227 ) ;
#100555=ORIENTED_EDGE ( 'NONE', *, *, #3588, .F. ) ;
#100559=DIRECTION ( 'NONE',  ( -0.7071067811865486830, -0.7071067811865464625, 0.000000000000000000 ) ) ;
#100560=DIRECTION ( 'NONE',  ( -0.6830127018922180770, -0.6830127018922204085, -0.2588190451025213501 ) ) ;
#100561=ADVANCED_FACE ( 'NONE', ( #37586 ), #115086, .T. ) ;
#100562=DIRECTION ( 'NONE',  ( 0.7071067811865487940, 0.7071067811865463515, -0.000000000000000000 ) ) ;
#100563=DIRECTION ( 'NONE',  ( -0.7071067811865487940, 0.7071067811865463515, 0.000000000000000000 ) ) ;
#100564=EDGE_CURVE ( 'NONE', #8692, #58822, #28853, .T. ) ;
#100566=CARTESIAN_POINT ( 'NONE',  ( -14.99451991528749595, 28.92564299267948513, 4.000000000000000000 ) ) ;
#100567=DIRECTION ( 'NONE',  ( -0.7071067811865486830, -0.7071067811865464625, -0.000000000000000000 ) ) ;
#100568=CARTESIAN_POINT ( 'NONE',  ( -30.18398860626900060, 28.73617430169808173, 5.000000000000000000 ) ) ;
#100574=CARTESIAN_POINT ( 'NONE',  ( 54.48921356237310221, -27.52281430457093236, 5.000000000000000000 ) ) ;
#100575=CARTESIAN_POINT ( 'NONE',  ( 10.49999999999991829, -12.08601207473288675, -10.46905243149096698 ) ) ;
#100576=ORIENTED_EDGE ( 'NONE', *, *, #112457, .T. ) ;
#100578=ADVANCED_FACE ( 'NONE', ( #112978 ), #57933, .T. ) ;
#100579=DIRECTION ( 'NONE',  ( -0.7071067811865486830, -0.7071067811865464625, -0.000000000000000000 ) ) ;
#100580=ORIENTED_EDGE ( 'NONE', *, *, #125053, .T. ) ;
#100583=DIRECTION ( 'NONE',  ( 0.6830127018922180770, -0.6830127018922204085, -0.2588190451025213501 ) ) ;
#100584=VERTEX_POINT ( 'NONE', #106355 ) ;
#100585=( BOUNDED_CURVE ( )  B_SPLINE_CURVE ( 3, ( #9193, #107118, #97677, #143324 ),
 .UNSPECIFIED., .F., .F. ) 
 B_SPLINE_CURVE_WITH_KNOTS ( ( 4, 4 ),
 ( 1.208578181583239486, 1.359146454359484890 ),
 .UNSPECIFIED. ) 
 CURVE ( )  GEOMETRIC_REPRESENTATION_ITEM ( )  RATIONAL_B_SPLINE_CURVE ( ( 1.000000000000000000, 0.9981116584018941973, 0.9981116584018941973, 1.000000000000000000 ) ) 
 REPRESENTATION_ITEM ( '' )  );
#100587=CARTESIAN_POINT ( 'NONE',  ( 28.82816939922333432, -5.240707523384228850, 4.000000000000000000 ) ) ;
#100590=VECTOR ( 'NONE', #46742, 1000.000000000000000 ) ;
#100591=VECTOR ( 'NONE', #96229, 1000.000000000000000 ) ;
#100592=FACE_OUTER_BOUND ( 'NONE', #125813, .T. ) ;
#100593=ORIENTED_EDGE ( 'NONE', *, *, #3055, .F. ) ;
#100594=CARTESIAN_POINT ( 'NONE',  ( -18.70710678118641113, 14.25929247661557397, 5.000000000000000000 ) ) ;
#100595=DIRECTION ( 'NONE',  ( -0.000000000000000000, -0.3543493200069152693, 0.9351131265310292928 ) ) ;
#100596=LINE ( 'NONE', #70145, #99323 ) ;
#100598=LINE ( 'NONE', #68692, #7449 ) ;
#100599=CARTESIAN_POINT ( 'NONE',  ( 11.24139925780195171, 21.72500000000000142, 5.000000000000000000 ) ) ;
#100600=DIRECTION ( 'NONE',  ( 0.3543493200069163795, -9.265275131829747941E-33, -0.9351131265310288487 ) ) ;
#100601=ORIENTED_EDGE ( 'NONE', *, *, #65646, .T. ) ;
#100603=VECTOR ( 'NONE', #37381, 1000.000000000000227 ) ;
#100604=PLANE ( 'NONE',  #90723 ) ;
#100605=ORIENTED_EDGE ( 'NONE', *, *, #8448, .T. ) ;
#100607=CARTESIAN_POINT ( 'NONE',  ( 24.48921356237309510, -27.52281430457072631, 5.000000000000000000 ) ) ;
#100608=CARTESIAN_POINT ( 'NONE',  ( 32.99999999999976552, -0.03360074219773898085, 5.000000000000000000 ) ) ;
#100610=LINE ( 'NONE', #34629, #142784 ) ;
#100611=ORIENTED_EDGE ( 'NONE', *, *, #70273, .F. ) ;
#100612=DIRECTION ( 'NONE',  ( 1.000000000000000000, 0.000000000000000000, 0.000000000000000000 ) ) ;
#100613=CARTESIAN_POINT ( 'NONE',  ( 80.99451991528748351, 28.92564299267994699, 4.000000000000000000 ) ) ;
#100614=CARTESIAN_POINT ( 'NONE',  ( 5.207106781186514155, 3.759292476615676559, 5.000000000000000000 ) ) ;
#100615=DIRECTION ( 'NONE',  ( -0.7071067811865486830, -0.7071067811865464625, -0.000000000000000000 ) ) ;
#100616=LINE ( 'NONE', #22289, #70671 ) ;
#100617=ORIENTED_EDGE ( 'NONE', *, *, #94692, .F. ) ;
#100619=CARTESIAN_POINT ( 'NONE',  ( 0.000000000000000000, 0.000000000000000000, 5.000000000000000000 ) ) ;
#100620=CARTESIAN_POINT ( 'NONE',  ( -6.183988606268994381, 28.73617430169791476, 5.000000000000000000 ) ) ;
#100621=DIRECTION ( 'NONE',  ( -0.7071067811865487940, 0.7071067811865463515, -0.000000000000000000 ) ) ;
#100622=CARTESIAN_POINT ( 'NONE',  ( 19.49999999999985789, -2.777013188829488666, 4.549262955118046570 ) ) ;
#100623=ORIENTED_EDGE ( 'NONE', *, *, #61229, .F. ) ;
#100624=VERTEX_POINT ( 'NONE', #52710 ) ;
#100625=VERTEX_POINT ( 'NONE', #127422 ) ;
#100626=ADVANCED_FACE ( 'NONE', ( #129560 ), #72389, .F. ) ;
#100628=VERTEX_POINT ( 'NONE', #38997 ) ;
#100630=DIRECTION ( 'NONE',  ( 0.7071067811865486830, -0.7071067811865464625, -0.000000000000000000 ) ) ;
#100631=CARTESIAN_POINT ( 'NONE',  ( 14.92733143757284786, -1.141545485034857643, 4.000000000000000000 ) ) ;
#100632=EDGE_CURVE ( 'NONE', #17012, #123516, #40449, .T. ) ;
#100633=DIRECTION ( 'NONE',  ( -0.6830127018922181881, 0.6830127018922202975, -0.2588190451025214056 ) ) ;
#100634=DIRECTION ( 'NONE',  ( -0.7071067811865486830, -0.7071067811865464625, 0.000000000000000000 ) ) ;
#100635=ORIENTED_EDGE ( 'NONE', *, *, #51219, .T. ) ;
#100636=ADVANCED_FACE ( 'NONE', ( #52020 ), #94779, .F. ) ;
#100637=DIRECTION ( 'NONE',  ( 0.3543493200069162685, -0.000000000000000000, -0.9351131265310288487 ) ) ;
#100638=DIRECTION ( 'NONE',  ( -0.7071067811865487940, 0.7071067811865463515, -0.000000000000000000 ) ) ;
#100640=CARTESIAN_POINT ( 'NONE',  ( -30.29974487139158867, -27.71228299555227537, 4.000000000000000000 ) ) ;
#100643=CARTESIAN_POINT ( 'NONE',  ( 32.99999999999977263, 4.931123077392136622, 4.000000000000000000 ) ) ;
#100644=DIRECTION ( 'NONE',  ( -0.6830127018922181881, 0.6830127018922202975, -0.2588190451025214056 ) ) ;
#100645=EDGE_LOOP ( 'NONE', ( #70826, #17039, #348, #120404 ) ) ;
#100646=ORIENTED_EDGE ( 'NONE', *, *, #122470, .T. ) ;
#100648=DIRECTION ( 'NONE',  ( -0.7071067811865487940, 0.7071067811865463515, 0.000000000000000000 ) ) ;
#100649=ADVANCED_FACE ( 'NONE', ( #104955 ), #126696, .T. ) ;
#100650=CARTESIAN_POINT ( 'NONE',  ( -31.49999999999976552, 19.08746187583905041, 4.000000000000000000 ) ) ;
#100652=CARTESIAN_POINT ( 'NONE',  ( -28.49999999999980460, 13.46639925780212721, 5.000000000000000000 ) ) ;
#100653=VECTOR ( 'NONE', #17573, 1000.000000000000000 ) ;
#100654=LINE ( 'NONE', #77491, #66521 ) ;
#100655=EDGE_CURVE ( 'NONE', #29435, #26904, #61503, .T. ) ;
#100656=LINE ( 'NONE', #69467, #99731 ) ;
#100657=FACE_OUTER_BOUND ( 'NONE', #78363, .T. ) ;
#100658=VECTOR ( 'NONE', #5713, 1000.000000000000114 ) ;
#100659=ORIENTED_EDGE ( 'NONE', *, *, #120341, .F. ) ;
#100660=VERTEX_POINT ( 'NONE', #94076 ) ;
#100661=VECTOR ( 'NONE', #98956, 999.9999999999998863 ) ;
#100662=LINE ( 'NONE', #99186, #105805 ) ;
#100663=ORIENTED_EDGE ( 'NONE', *, *, #108275, .T. ) ;
#100664=EDGE_LOOP ( 'NONE', ( #96944, #94405, #106562, #84602 ) ) ;
#100665=ADVANCED_FACE ( 'NONE', ( #19381 ), #49899, .F. ) ;
#100666=PLANE ( 'NONE',  #42759 ) ;
#100667=ORIENTED_EDGE ( 'NONE', *, *, #12056, .F. ) ;
#100668=CARTESIAN_POINT ( 'NONE',  ( -11.99999999999991296, -0.8619312979532105512, -5.102805207349851990 ) ) ;
#100669=DIRECTION ( 'NONE',  ( -0.7071067811865486830, -0.7071067811865464625, -0.000000000000000000 ) ) ;
#100670=ADVANCED_FACE ( 'NONE', ( #39736 ), #139031, .F. ) ;
#100671=CARTESIAN_POINT ( 'NONE',  ( 2.671830600776447628, 14.25929247661557575, 4.000000000000000000 ) ) ;
#100672=CARTESIAN_POINT ( 'NONE',  ( 0.000000000000000000, 0.000000000000000000, 5.000000000000000000 ) ) ;
#100673=ORIENTED_EDGE ( 'NONE', *, *, #33505, .F. ) ;
#100675=VERTEX_POINT ( 'NONE', #28123 ) ;
#100676=CARTESIAN_POINT ( 'NONE',  ( -20.51078643762690490, -27.52281430457041012, 5.000000000000000000 ) ) ;
#100677=ORIENTED_EDGE ( 'NONE', *, *, #141765, .T. ) ;
#100678=CARTESIAN_POINT ( 'NONE',  ( 0.000000000000000000, 0.000000000000000000, 5.000000000000000000 ) ) ;
#100679=EDGE_LOOP ( 'NONE', ( #34039, #129787, #116138, #86926 ) ) ;
#100680=LINE ( 'NONE', #36830, #64438 ) ;
#100682=VERTEX_POINT ( 'NONE', #83221 ) ;
#100684=ADVANCED_FACE ( 'NONE', ( #139765 ), #117236, .F. ) ;
#100685=VECTOR ( 'NONE', #103949, 999.9999999999998863 ) ;
#100686=CARTESIAN_POINT ( 'NONE',  ( -7.171830600776416986, 15.75929247661555976, 4.000000000000000000 ) ) ;
#100687=AXIS2_PLACEMENT_3D ( 'NONE', #68997, #67582, #113175 ) ;
#100688=CARTESIAN_POINT ( 'NONE',  ( 0.4892135623730947680, -27.52281430457055578, 5.000000000000000000 ) ) ;
#100691=DIRECTION ( 'NONE',  ( 0.7071067811865487940, 0.7071067811865463515, 0.000000000000000000 ) ) ;
#100694=DIRECTION ( 'NONE',  ( 0.3543493200069162685, -0.000000000000000000, -0.9351131265310288487 ) ) ;
#100695=PLANE ( 'NONE',  #31071 ) ;
#100696=DIRECTION ( 'NONE',  ( -0.000000000000000000, -0.3543493200069152693, 0.9351131265310292928 ) ) ;
#100697=DIRECTION ( 'NONE',  ( -0.7071067811865487940, 0.7071067811865463515, -0.000000000000000000 ) ) ;
#100700=CARTESIAN_POINT ( 'NONE',  ( 18.18398860626898994, 28.73617430169800002, 5.000000000000000000 ) ) ;
#100701=DIRECTION ( 'NONE',  ( -0.6830127018922180770, -0.6830127018922204085, -0.2588190451025214056 ) ) ;
#100702=EDGE_CURVE ( 'NONE', #75355, #10476, #51312, .T. ) ;
#100703=ORIENTED_EDGE ( 'NONE', *, *, #136575, .T. ) ;
#100704=ORIENTED_EDGE ( 'NONE', *, *, #16984, .F. ) ;
#100705=PLANE ( 'NONE',  #109686 ) ;
#100706=ORIENTED_EDGE ( 'NONE', *, *, #68404, .F. ) ;
#100707=ORIENTED_EDGE ( 'NONE', *, *, #29386, .T. ) ;
#100708=CARTESIAN_POINT ( 'NONE',  ( 48.18398860626899705, 28.73617430169820608, 5.000000000000000000 ) ) ;
#100709=CARTESIAN_POINT ( 'NONE',  ( -12.18398860626900060, 28.73617430169795739, 5.000000000000000000 ) ) ;
#100710=DIRECTION ( 'NONE',  ( -0.000000000000000000, 0.3543493200069153248, 0.9351131265310292928 ) ) ;
#100711=EDGE_CURVE ( 'NONE', #34037, #33763, #42843, .T. ) ;
#100712=LINE ( 'NONE', #90551, #125054 ) ;
#100713=FACE_OUTER_BOUND ( 'NONE', #38278, .T. ) ;
#100714=ORIENTED_EDGE ( 'NONE', *, *, #113823, .F. ) ;
#100715=FACE_OUTER_BOUND ( 'NONE', #40075, .T. ) ;
#100716=ORIENTED_EDGE ( 'NONE', *, *, #23726, .T. ) ;
#100719=VERTEX_POINT ( 'NONE', #41131 ) ;
#100722=VERTEX_POINT ( 'NONE', #64322 ) ;
#100723=ORIENTED_EDGE ( 'NONE', *, *, #118057, .T. ) ;
#100724=ORIENTED_EDGE ( 'NONE', *, *, #79755, .T. ) ;
#100725=DIRECTION ( 'NONE',  ( 0.7071067811865487940, 0.7071067811865463515, 0.000000000000000000 ) ) ;
#100726=PLANE ( 'NONE',  #129601 ) ;
#100727=CARTESIAN_POINT ( 'NONE',  ( -3.793339364578453665, 21.75929247661549581, 4.998822639870701856 ) ) ;
#100728=DIRECTION ( 'NONE',  ( -0.000000000000000000, 0.000000000000000000, 1.000000000000000000 ) ) ;
#100729=EDGE_LOOP ( 'NONE', ( #110361, #96724, #16308, #70494 ) ) ;
#100730=ADVANCED_FACE ( 'NONE', ( #131722 ), #44002, .F. ) ;
#100731=CARTESIAN_POINT ( 'NONE',  ( -21.18398860626899349, 28.73617430169802134, 5.000000000000000000 ) ) ;
#100734=CARTESIAN_POINT ( 'NONE',  ( 8.994519915287490619, 28.92564299267944250, 4.000000000000000000 ) ) ;
#100737=ADVANCED_FACE ( 'NONE', ( #88221 ), #67180, .F. ) ;
#100738=DIRECTION ( 'NONE',  ( -0.7071067811865486830, -0.7071067811865464625, 0.000000000000000000 ) ) ;
#100740=ORIENTED_EDGE ( 'NONE', *, *, #51253, .T. ) ;
#100741=EDGE_CURVE ( 'NONE', #55203, #134557, #20075, .T. ) ;
#100743=ORIENTED_EDGE ( 'NONE', *, *, #71161, .T. ) ;
#100745=DIRECTION ( 'NONE',  ( 0.7071067811865486830, -0.7071067811865464625, -0.000000000000000000 ) ) ;
#100746=CARTESIAN_POINT ( 'NONE',  ( 8.999999999999937828, -6.108550654416951886, -3.114665004254947078 ) ) ;
#100747=VECTOR ( 'NONE', #87586, 1000.000000000000227 ) ;
#100748=LINE ( 'NONE', #1399, #11417 ) ;
#100749=CARTESIAN_POINT ( 'NONE',  ( -34.92500000000001137, 22.22500000000000142, 4.000000000000000000 ) ) ;
#100750=VECTOR ( 'NONE', #44090, 1000.000000000000000 ) ;
#100751=DIRECTION ( 'NONE',  ( 0.7071067811865487940, 0.7071067811865463515, 0.000000000000000000 ) ) ;
#100752=CARTESIAN_POINT ( 'NONE',  ( -34.92500000000001137, 22.22500000000000142, 4.500000000000000888 ) ) ;
#100753=DIRECTION ( 'NONE',  ( -0.3543493200069162685, -0.000000000000000000, -0.9351131265310288487 ) ) ;
#100754=CARTESIAN_POINT ( 'NONE',  ( -24.29974487139158867, -27.71228299555223273, 4.000000000000000000 ) ) ;
#100757=CARTESIAN_POINT ( 'NONE',  ( 12.48921356237309155, -27.52281430457064104, 5.000000000000000000 ) ) ;
#100758=DIRECTION ( 'NONE',  ( 0.3543493200069162685, -0.000000000000000000, -0.9351131265310288487 ) ) ;
#100759=DIRECTION ( 'NONE',  ( 1.000000000000000000, 0.000000000000000000, 0.000000000000000000 ) ) ;
#100760=VERTEX_POINT ( 'NONE', #54196 ) ;
#100761=ADVANCED_FACE ( 'NONE', ( #108489 ), #53436, .F. ) ;
#100762=ORIENTED_EDGE ( 'NONE', *, *, #73087, .T. ) ;
#100765=VECTOR ( 'NONE', #117301, 999.9999999999998863 ) ;
#100766=VERTEX_POINT ( 'NONE', #77372 ) ;
#100767=ORIENTED_EDGE ( 'NONE', *, *, #25151, .T. ) ;
#100768=LINE ( 'NONE', #134122, #84988 ) ;
#100770=DIRECTION ( 'NONE',  ( -0.6830127018922180770, -0.6830127018922204085, -0.2588190451025213501 ) ) ;
#100771=ORIENTED_EDGE ( 'NONE', *, *, #97353, .T. ) ;
#100772=PLANE ( 'NONE',  #2335 ) ;
#100774=CARTESIAN_POINT ( 'NONE',  ( -16.83455439249994612, 8.717631302929021331, 5.000000000000000000 ) ) ;
#100776=ORIENTED_EDGE ( 'NONE', *, *, #117625, .T. ) ;
#100778=LINE ( 'NONE', #98109, #107202 ) ;
#100780=CARTESIAN_POINT ( 'NONE',  ( -18.18398860626898994, 28.73617430169800002, 5.000000000000000000 ) ) ;
#100781=CARTESIAN_POINT ( 'NONE',  ( 34.49999999999976552, 10.08746187583914100, 4.000000000000000000 ) ) ;
#100782=CARTESIAN_POINT ( 'NONE',  ( 24.99033360189226016, 3.759292476615681888, 4.478963035907999490 ) ) ;
#100783=LINE ( 'NONE', #135568, #68621 ) ;
#100786=AXIS2_PLACEMENT_3D ( 'NONE', #66305, #101763, #22048 ) ;
#100787=VERTEX_POINT ( 'NONE', #75910 ) ;
#100789=VECTOR ( 'NONE', #111666, 1000.000000000000000 ) ;
#100790=ADVANCED_FACE ( 'NONE', ( #122243 ), #31692, .F. ) ;
#100792=ORIENTED_EDGE ( 'NONE', *, *, #68754, .T. ) ;
#100793=AXIS2_PLACEMENT_3D ( 'NONE', #20234, #64479, #87658 ) ;
#100794=ADVANCED_FACE ( 'NONE', ( #119383 ), #12060, .T. ) ;
#100795=CARTESIAN_POINT ( 'NONE',  ( 7.828169399223472880, 15.75929247661555976, 4.000000000000000000 ) ) ;
#100797=EDGE_CURVE ( 'NONE', #55578, #59038, #55600, .T. ) ;
#100798=EDGE_CURVE ( 'NONE', #118739, #109940, #462, .T. ) ;
#100799=CARTESIAN_POINT ( 'NONE',  ( 18.18398860626898994, 28.73617430169800002, 5.000000000000000000 ) ) ;
#100800=DIRECTION ( 'NONE',  ( 0.7071067811865486830, -0.7071067811865464625, -0.000000000000000000 ) ) ;
#100802=VERTEX_POINT ( 'NONE', #130311 ) ;
#100803=ORIENTED_EDGE ( 'NONE', *, *, #13422, .F. ) ;
#100804=DIRECTION ( 'NONE',  ( -0.7071067811865486830, -0.7071067811865464625, -0.000000000000000000 ) ) ;
#100805=ORIENTED_EDGE ( 'NONE', *, *, #40975, .T. ) ;
#100806=EDGE_LOOP ( 'NONE', ( #63377, #77068, #85695, #136755 ) ) ;
#100808=ADVANCED_FACE ( 'NONE', ( #30998 ), #66478, .T. ) ;
#100809=EDGE_LOOP ( 'NONE', ( #31657, #38175, #2113, #92610 ) ) ;
#100810=CARTESIAN_POINT ( 'NONE',  ( -5.999999999999963585, -5.527737879153202805, -7.983877177622358268 ) ) ;
#100811=EDGE_CURVE ( 'NONE', #129125, #134614, #22215, .T. ) ;
#100813=EDGE_CURVE ( 'NONE', #139420, #27206, #109242, .T. ) ;
#100814=CARTESIAN_POINT ( 'NONE',  ( -34.49999999999975842, 16.46425560840032176, 4.994342998332164107 ) ) ;
#100815=ORIENTED_EDGE ( 'NONE', *, *, #76948, .T. ) ;
#100816=CARTESIAN_POINT ( 'NONE',  ( -42.18398860626899705, 28.73617430169816700, 5.000000000000000000 ) ) ;
#100817=ORIENTED_EDGE ( 'NONE', *, *, #60791, .T. ) ;
#100818=ORIENTED_EDGE ( 'NONE', *, *, #82015, .T. ) ;
#100820=ORIENTED_EDGE ( 'NONE', *, *, #53964, .T. ) ;
#100821=CARTESIAN_POINT ( 'NONE',  ( 29.99999999999978328, -16.02097659208068947, -11.96015758381215655 ) ) ;
#100824=PLANE ( 'NONE',  #87712 ) ;
#100826=EDGE_CURVE ( 'NONE', #40283, #116562, #21531, .T. ) ;
#100828=LINE ( 'NONE', #43591, #95279 ) ;
#100829=FACE_BOUND ( 'NONE', #69717, .T. ) ;
#100830=ORIENTED_EDGE ( 'NONE', *, *, #48101, .T. ) ;
#100831=DIRECTION ( 'NONE',  ( -0.7071067811865486830, -0.7071067811865464625, 0.000000000000000000 ) ) ;
#100832=CARTESIAN_POINT ( 'NONE',  ( -8.816011393731004731, 28.73617430169781173, 5.000000000000000000 ) ) ;
#100833=FACE_OUTER_BOUND ( 'NONE', #43500, .T. ) ;
#100834=CARTESIAN_POINT ( 'NONE',  ( 17.99999999999986855, -19.06887692260762179, 4.000000000000000000 ) ) ;
#100835=ORIENTED_EDGE ( 'NONE', *, *, #135338, .T. ) ;
#100836=ADVANCED_FACE ( 'NONE', ( #54889 ), #99056, .T. ) ;
#100838=ORIENTED_EDGE ( 'NONE', *, *, #110062, .F. ) ;
#100839=ADVANCED_FACE ( 'NONE', ( #14915 ), #91091, .F. ) ;
#100840=VERTEX_POINT ( 'NONE', #125112 ) ;
#100841=VERTEX_POINT ( 'NONE', #48267 ) ;
#100843=VECTOR ( 'NONE', #129306, 1000.000000000000227 ) ;
#100845=ORIENTED_EDGE ( 'NONE', *, *, #47212, .T. ) ;
#100846=CARTESIAN_POINT ( 'NONE',  ( -19.49999999999987210, 1.030536316426487797, -5.498701923753756660 ) ) ;
#100847=DIRECTION ( 'NONE',  ( -0.7071067811865486830, -0.7071067811865464625, -0.000000000000000000 ) ) ;
#100848=VERTEX_POINT ( 'NONE', #135993 ) ;
#100849=CARTESIAN_POINT ( 'NONE',  ( -9.328169399223456892, -15.74070752338412049, 4.000000000000000000 ) ) ;
#100850=DIRECTION ( 'NONE',  ( 0.7071067811865487940, 0.7071067811865463515, 0.000000000000000000 ) ) ;
#100851=DIRECTION ( 'NONE',  ( -0.7071067811865486830, -0.7071067811865464625, 0.000000000000000000 ) ) ;
#100853=CARTESIAN_POINT ( 'NONE',  ( -20.99451991528748707, 28.92564299267952777, 4.000000000000000000 ) ) ;
#100854=CARTESIAN_POINT ( 'NONE',  ( 27.41161490594811667, 22.22500000000000142, 4.777194822843816802 ) ) ;
#100855=PLANE ( 'NONE',  #51697 ) ;
#100856=ORIENTED_EDGE ( 'NONE', *, *, #87043, .F. ) ;
#100857=ORIENTED_EDGE ( 'NONE', *, *, #74603, .F. ) ;
#100858=EDGE_LOOP ( 'NONE', ( #8306, #26454, #65076, #17775 ) ) ;
#100859=ORIENTED_EDGE ( 'NONE', *, *, #70884, .F. ) ;
#100860=LINE ( 'NONE', #90727, #98275 ) ;
#100862=ORIENTED_EDGE ( 'NONE', *, *, #10281, .T. ) ;
#100863=VERTEX_POINT ( 'NONE', #102673 ) ;
#100865=CARTESIAN_POINT ( 'NONE',  ( -57.29974487139158157, -27.71228299555246011, 4.000000000000000000 ) ) ;
#100866=VERTEX_POINT ( 'NONE', #122984 ) ;
#100867=DIRECTION ( 'NONE',  ( 0.6830127018922180770, -0.6830127018922204085, -0.2588190451025213501 ) ) ;
#100868=VECTOR ( 'NONE', #118609, 1000.000000000000227 ) ;
#100869=CARTESIAN_POINT ( 'NONE',  ( 14.81601139373099585, 28.73617430169776910, 5.000000000000000000 ) ) ;
#100871=AXIS2_PLACEMENT_3D ( 'NONE', #91536, #124150, #135068 ) ;
#100872=DIRECTION ( 'NONE',  ( 0.7071067811865487940, -0.7071067811865463515, 0.000000000000000000 ) ) ;
#100873=ORIENTED_EDGE ( 'NONE', *, *, #17194, .T. ) ;
#100875=FACE_OUTER_BOUND ( 'NONE', #83593, .T. ) ;
#100876=VECTOR ( 'NONE', #61686, 1000.000000000000227 ) ;
#100877=CARTESIAN_POINT ( 'NONE',  ( 0.000000000000000000, 0.000000000000000000, 5.000000000000000000 ) ) ;
#100878=CARTESIAN_POINT ( 'NONE',  ( -36.51168605928409505, 6.759292476615653023, 16.35960578974477997 ) ) ;
#100879=CARTESIAN_POINT ( 'NONE',  ( -11.29289321881338104, -0.7407075233842770334, 5.000000000000000000 ) ) ;
#100881=VERTEX_POINT ( 'NONE', #67936 ) ;
#100882=CARTESIAN_POINT ( 'NONE',  ( -63.18398860626900415, 28.73617430169831621, 5.000000000000000000 ) ) ;
#100884=VECTOR ( 'NONE', #118564, 1000.000000000000000 ) ;
#100888=ORIENTED_EDGE ( 'NONE', *, *, #89518, .T. ) ;
#100892=VERTEX_POINT ( 'NONE', #125853 ) ;
#100893=LINE ( 'NONE', #132125, #53876 ) ;
#100895=LINE ( 'NONE', #68321, #85467 ) ;
#100896=ADVANCED_FACE ( 'NONE', ( #2604 ), #3992, .F. ) ;
#100898=ORIENTED_EDGE ( 'NONE', *, *, #117573, .F. ) ;
#100899=EDGE_CURVE ( 'NONE', #52088, #131561, #36669, .T. ) ;
#100900=EDGE_LOOP ( 'NONE', ( #9479, #137863, #58059, #49812 ) ) ;
#100901=CARTESIAN_POINT ( 'NONE',  ( 0.3281693992235323876, 11.25929247661561305, 4.000000000000000000 ) ) ;
#100902=DIRECTION ( 'NONE',  ( -0.000000000000000000, 0.3543493200069153248, 0.9351131265310292928 ) ) ;
#100903=ORIENTED_EDGE ( 'NONE', *, *, #41847, .F. ) ;
#100904=CARTESIAN_POINT ( 'NONE',  ( 59.99451991528749772, 28.92564299267980132, 4.000000000000000000 ) ) ;
#100905=DIRECTION ( 'NONE',  ( 0.7071067811865487940, 0.7071067811865463515, 0.000000000000000000 ) ) ;
#100907=VERTEX_POINT ( 'NONE', #25071 ) ;
#100908=EDGE_CURVE ( 'NONE', #93195, #56372, #37402, .T. ) ;
#100909=DIRECTION ( 'NONE',  ( -0.000000000000000000, -0.3543493200069152693, 0.9351131265310292928 ) ) ;
#100910=CARTESIAN_POINT ( 'NONE',  ( -18.18398860626898994, 28.73617430169800002, 5.000000000000000000 ) ) ;
#100911=DIRECTION ( 'NONE',  ( -0.3543493200069162685, -0.000000000000000000, -0.9351131265310288487 ) ) ;
#100913=CARTESIAN_POINT ( 'NONE',  ( 9.792893218813389922, 3.759292476615674783, 5.000000000000000000 ) ) ;
#100915=DIRECTION ( 'NONE',  ( -0.7071067811865486830, -0.7071067811865464625, -0.000000000000000000 ) ) ;
#100916=ORIENTED_EDGE ( 'NONE', *, *, #21463, .F. ) ;
#100917=EDGE_CURVE ( 'NONE', #28997, #34677, #26525, .T. ) ;
#100918=ORIENTED_EDGE ( 'NONE', *, *, #28333, .F. ) ;
#100919=ORIENTED_EDGE ( 'NONE', *, *, #26524, .T. ) ;
#100920=DIRECTION ( 'NONE',  ( -0.7071067811865486830, -0.7071067811865464625, 0.000000000000000000 ) ) ;
#100921=VERTEX_POINT ( 'NONE', #112809 ) ;
#100922=ORIENTED_EDGE ( 'NONE', *, *, #51620, .F. ) ;
#100926=EDGE_CURVE ( 'NONE', #101563, #23274, #92466, .T. ) ;
#100927=ORIENTED_EDGE ( 'NONE', *, *, #8104, .F. ) ;
#100928=DIRECTION ( 'NONE',  ( 1.000000000000000000, -0.000000000000000000, 0.000000000000000000 ) ) ;
#100929=CARTESIAN_POINT ( 'NONE',  ( 0.000000000000000000, 0.000000000000000000, 5.000000000000000000 ) ) ;
#100930=FACE_OUTER_BOUND ( 'NONE', #3984, .T. ) ;
#100931=DIRECTION ( 'NONE',  ( 0.6830127018922181881, 0.6830127018922202975, -0.2588190451025214056 ) ) ;
#100933=ORIENTED_EDGE ( 'NONE', *, *, #9161, .F. ) ;
#100934=PLANE ( 'NONE',  #71946 ) ;
#100937=LINE ( 'NONE', #1594, #3954 ) ;
#100939=LINE ( 'NONE', #142332, #60814 ) ;
#100940=FACE_OUTER_BOUND ( 'NONE', #119588, .T. ) ;
#100942=VECTOR ( 'NONE', #75177, 1000.000000000000000 ) ;
#100943=CARTESIAN_POINT ( 'NONE',  ( 2.999999999999978240, -21.41253812416053748, 4.000000000000000000 ) ) ;
#100944=DIRECTION ( 'NONE',  ( 1.000000000000000000, 0.000000000000000000, 0.000000000000000000 ) ) ;
#100946=ORIENTED_EDGE ( 'NONE', *, *, #138932, .T. ) ;
#100948=VECTOR ( 'NONE', #97778, 1000.000000000000000 ) ;
#100949=LINE ( 'NONE', #88676, #59930 ) ;
#100952=LINE ( 'NONE', #109694, #101072 ) ;
#100953=DIRECTION ( 'NONE',  ( -0.7071067811865486830, 0.7071067811865464625, 0.000000000000000000 ) ) ;
#100954=EDGE_CURVE ( 'NONE', #75725, #42588, #114915, .T. ) ;
#100955=EDGE_CURVE ( 'NONE', #3311, #70705, #57045, .T. ) ;
#100957=VECTOR ( 'NONE', #102965, 1000.000000000000000 ) ;
#100958=ORIENTED_EDGE ( 'NONE', *, *, #23020, .F. ) ;
#100959=CARTESIAN_POINT ( 'NONE',  ( 14.99999999999989875, -1.209798855135680418, 4.371887122346866050 ) ) ;
#100960=ORIENTED_EDGE ( 'NONE', *, *, #80367, .T. ) ;
#100961=LINE ( 'NONE', #25542, #40363 ) ;
#100962=EDGE_CURVE ( 'NONE', #71933, #99127, #70074, .T. ) ;
#100964=LINE ( 'NONE', #11069, #113795 ) ;
#100965=CARTESIAN_POINT ( 'NONE',  ( -7.410090645198278203, 9.759292476615614831, 11.28811694763777140 ) ) ;
#100966=EDGE_LOOP ( 'NONE', ( #38926, #11375, #98, #10345, #130535 ) ) ;
#100967=VECTOR ( 'NONE', #92575, 999.9999999999998863 ) ;
#100969=DIRECTION ( 'NONE',  ( -0.7071067811865486830, -0.7071067811865464625, -0.000000000000000000 ) ) ;
#100970=ORIENTED_EDGE ( 'NONE', *, *, #111575, .F. ) ;
#100971=CARTESIAN_POINT ( 'NONE',  ( -8.999999999999941380, -6.108550654416969650, -3.114665004254987046 ) ) ;
#100973=DIRECTION ( 'NONE',  ( 0.7071067811865487940, 0.7071067811865463515, -0.000000000000000000 ) ) ;
#100977=VERTEX_POINT ( 'NONE', #12769 ) ;
#100978=EDGE_CURVE ( 'NONE', #138243, #22107, #101216, .T. ) ;
#100981=VECTOR ( 'NONE', #136255, 1000.000000000000000 ) ;
#100983=PLANE ( 'NONE',  #142690 ) ;
#100984=DIRECTION ( 'NONE',  ( -0.6830127018922180770, -0.6830127018922204085, -0.2588190451025213501 ) ) ;
#100985=VERTEX_POINT ( 'NONE', #134594 ) ;
#100986=VECTOR ( 'NONE', #110527, 1000.000000000000000 ) ;
#100988=ADVANCED_FACE ( 'NONE', ( #35291 ), #79533, .F. ) ;
#100989=ORIENTED_EDGE ( 'NONE', *, *, #112172, .F. ) ;
#100990=DIRECTION ( 'NONE',  ( 0.6830127018922181881, 0.6830127018922202975, -0.2588190451025214056 ) ) ;
#100992=DIRECTION ( 'NONE',  ( 0.7071067811865487940, 0.7071067811865463515, -0.000000000000000000 ) ) ;
#100993=CARTESIAN_POINT ( 'NONE',  ( 0.000000000000000000, 0.000000000000000000, 5.000000000000000000 ) ) ;
#100994=CARTESIAN_POINT ( 'NONE',  ( 1.499999999999990896, -12.66682484999666336, -0.6294897503863906563 ) ) ;
#100995=CARTESIAN_POINT ( 'NONE',  ( -23.51078643762690490, -27.52281430457038880, 5.000000000000000000 ) ) ;
#100996=FACE_BOUND ( 'NONE', #44483, .T. ) ;
#100997=CARTESIAN_POINT ( 'NONE',  ( -5.999999999999960032, -0.03360074219773551141, 5.000000000000000000 ) ) ;
#100999=CARTESIAN_POINT ( 'NONE',  ( 63.29974487139158867, -27.71228299555250274, 4.000000000000000000 ) ) ;
#101001=ORIENTED_EDGE ( 'NONE', *, *, #109635, .T. ) ;
#101002=DIRECTION ( 'NONE',  ( -0.7071067811865486830, 0.7071067811865464625, 0.000000000000000000 ) ) ;
#101003=VERTEX_POINT ( 'NONE', #61340 ) ;
#101004=ADVANCED_FACE ( 'NONE', ( #84493 ), #19213, .F. ) ;
#101005=EDGE_CURVE ( 'NONE', #76368, #13267, #93909, .T. ) ;
#101006=VERTEX_POINT ( 'NONE', #27949 ) ;
#101008=ORIENTED_EDGE ( 'NONE', *, *, #38013, .F. ) ;
#101009=EDGE_CURVE ( 'NONE', #100121, #58114, #94612, .T. ) ;
#101010=DIRECTION ( 'NONE',  ( 0.7071067811865487940, 0.7071067811865463515, -0.000000000000000000 ) ) ;
#101011=ORIENTED_EDGE ( 'NONE', *, *, #107462, .T. ) ;
#101012=CARTESIAN_POINT ( 'NONE',  ( -47.99451991528749062, 28.92564299267971251, 4.000000000000000000 ) ) ;
#101013=VECTOR ( 'NONE', #135741, 999.9999999999998863 ) ;
#101014=DIRECTION ( 'NONE',  ( -0.6830127018922180770, -0.6830127018922204085, -0.2588190451025213501 ) ) ;
#101015=CARTESIAN_POINT ( 'NONE',  ( 3.781626882924918220, 21.74787736706806385, 4.999607392498048419 ) ) ;
#101017=CARTESIAN_POINT ( 'NONE',  ( 27.18398860626900060, 28.73617430169806042, 5.000000000000000000 ) ) ;
#101020=CARTESIAN_POINT ( 'NONE',  ( -34.92500000000001137, 22.22500000000000142, 4.000000000000000000 ) ) ;
#101021=ORIENTED_EDGE ( 'NONE', *, *, #71464, .F. ) ;
#101023=ORIENTED_EDGE ( 'NONE', *, *, #96736, .T. ) ;
#101024=DIRECTION ( 'NONE',  ( -0.7071067811865487940, 0.7071067811865463515, -0.000000000000000000 ) ) ;
#101025=DIRECTION ( 'NONE',  ( 0.3543493200069162685, -0.000000000000000000, -0.9351131265310288487 ) ) ;
#101026=VERTEX_POINT ( 'NONE', #4704 ) ;
#101029=DIRECTION ( 'NONE',  ( -0.000000000000000000, 0.000000000000000000, 1.000000000000000000 ) ) ;
#101030=VERTEX_POINT ( 'NONE', #74327 ) ;
#101031=DIRECTION ( 'NONE',  ( 0.7071067811865487940, -0.7071067811865463515, 0.000000000000000000 ) ) ;
#101032=VECTOR ( 'NONE', #131521, 1000.000000000000000 ) ;
#101033=PLANE ( 'NONE',  #53994 ) ;
#101035=PLANE ( 'NONE',  #100518 ) ;
#101036=VERTEX_POINT ( 'NONE', #115624 ) ;
#101037=VECTOR ( 'NONE', #139721, 1000.000000000000000 ) ;
#101038=LINE ( 'NONE', #45984, #133721 ) ;
#101039=DIRECTION ( 'NONE',  ( -1.000000000000000000, 0.000000000000000000, 0.000000000000000000 ) ) ;
#101040=EDGE_CURVE ( 'NONE', #23492, #34867, #118516, .T. ) ;
#101041=CARTESIAN_POINT ( 'NONE',  ( -25.01899999999999835, 3.174999999999998046, 5.000000000000000000 ) ) ;
#101042=CARTESIAN_POINT ( 'NONE',  ( -0.4892135623730947680, -27.52281430457055578, 5.000000000000000000 ) ) ;
#101043=VERTEX_POINT ( 'NONE', #73603 ) ;
#101044=EDGE_LOOP ( 'NONE', ( #118654, #70959, #105205, #82998 ) ) ;
#101046=DIRECTION ( 'NONE',  ( -0.000000000000000000, 0.3543493200069153248, 0.9351131265310292928 ) ) ;
#101047=LINE ( 'NONE', #101771, #61092 ) ;
#101051=CARTESIAN_POINT ( 'NONE',  ( -18.18398860626898994, 28.73617430169800002, 5.000000000000000000 ) ) ;
#101052=FACE_OUTER_BOUND ( 'NONE', #37278, .T. ) ;
#101053=FACE_OUTER_BOUND ( 'NONE', #139977, .T. ) ;
#101056=CARTESIAN_POINT ( 'NONE',  ( -19.49999999999985789, -5.947814304570772315, 5.000000000000000000 ) ) ;
#101057=EDGE_CURVE ( 'NONE', #106956, #85580, #60619, .T. ) ;
#101058=LINE ( 'NONE', #35133, #84146 ) ;
#101060=DIRECTION ( 'NONE',  ( 0.000000000000000000, -0.000000000000000000, 1.000000000000000000 ) ) ;
#101061=EDGE_CURVE ( 'NONE', #17266, #20431, #6151, .T. ) ;
#101062=EDGE_CURVE ( 'NONE', #135705, #60317, #105487, .T. ) ;
#101063=EDGE_LOOP ( 'NONE', ( #18972, #40317, #91755, #107430 ) ) ;
#101064=VERTEX_POINT ( 'NONE', #93199 ) ;
#101066=LINE ( 'NONE', #35141, #100284 ) ;
#101067=VECTOR ( 'NONE', #43573, 1000.000000000000227 ) ;
#101069=ADVANCED_FACE ( 'NONE', ( #50428 ), #138868, .F. ) ;
#101070=EDGE_CURVE ( 'NONE', #117324, #82150, #117078, .T. ) ;
#101071=CARTESIAN_POINT ( 'NONE',  ( 20.99999999999984723, -19.06887692260762179, 4.000000000000000000 ) ) ;
#101072=VECTOR ( 'NONE', #1611, 1000.000000000000000 ) ;
#101073=ORIENTED_EDGE ( 'NONE', *, *, #39142, .F. ) ;
#101074=DIRECTION ( 'NONE',  ( -0.6830127018922181881, 0.6830127018922202975, -0.2588190451025214056 ) ) ;
#101075=PLANE ( 'NONE',  #20543 ) ;
#101076=CARTESIAN_POINT ( 'NONE',  ( -15.18398860626900237, 28.73617430169797871, 5.000000000000000000 ) ) ;
#101077=ORIENTED_EDGE ( 'NONE', *, *, #21128, .T. ) ;
#101078=EDGE_CURVE ( 'NONE', #89322, #103729, #30075, .T. ) ;
#101083=VECTOR ( 'NONE', #46238, 1000.000000000000000 ) ;
#101086=CARTESIAN_POINT ( 'NONE',  ( 8.700255128608413102, -27.71228299555199825, 4.000000000000000000 ) ) ;
#101087=EDGE_CURVE ( 'NONE', #95318, #121873, #82350, .T. ) ;
#101088=PLANE ( 'NONE',  #85785 ) ;
#101089=CARTESIAN_POINT ( 'NONE',  ( 24.64327148205084939, 5.259292476615662792, 4.831541298974423526 ) ) ;
#101090=ORIENTED_EDGE ( 'NONE', *, *, #71416, .F. ) ;
#101091=CARTESIAN_POINT ( 'NONE',  ( 29.99451991528749417, 28.92564299267958816, 4.000000000000000000 ) ) ;
#101092=ADVANCED_FACE ( 'NONE', ( #95337 ), #39562, .F. ) ;
#101093=ORIENTED_EDGE ( 'NONE', *, *, #96635, .F. ) ;
#101095=ADVANCED_FACE ( 'NONE', ( #72218 ), #40972, .F. ) ;
#101096=DIRECTION ( 'NONE',  ( -0.7071067811865487940, 0.7071067811865463515, 0.000000000000000000 ) ) ;
#101097=FACE_OUTER_BOUND ( 'NONE', #16353, .T. ) ;
#101098=LINE ( 'NONE', #132351, #34694 ) ;
#101099=CARTESIAN_POINT ( 'NONE',  ( -5.999999999999956479, -8.731860332648846423, -2.120594902707551022 ) ) ;
#101100=CARTESIAN_POINT ( 'NONE',  ( 0.000000000000000000, 0.000000000000000000, 5.000000000000000000 ) ) ;
#101101=ORIENTED_EDGE ( 'NONE', *, *, #93430, .T. ) ;
#101102=ORIENTED_EDGE ( 'NONE', *, *, #67953, .T. ) ;
#101103=LINE ( 'NONE', #70666, #9247 ) ;
#101108=CARTESIAN_POINT ( 'NONE',  ( 21.70612307739180125, 22.22500000000000142, 4.000000000000000000 ) ) ;
#101110=CARTESIAN_POINT ( 'NONE',  ( 18.18398860626898994, 28.73617430169800002, 5.000000000000000000 ) ) ;
#101111=VECTOR ( 'NONE', #104969, 1000.000000000000000 ) ;
#101112=PLANE ( 'NONE',  #11230 ) ;
#101113=ORIENTED_EDGE ( 'NONE', *, *, #1847, .T. ) ;
#101115=LINE ( 'NONE', #109141, #104825 ) ;
#101116=FACE_OUTER_BOUND ( 'NONE', #68913, .T. ) ;
#101117=DIRECTION ( 'NONE',  ( -0.7071067811865487940, 0.7071067811865463515, 0.000000000000000000 ) ) ;
#101118=EDGE_CURVE ( 'NONE', #56866, #102894, #17756, .T. ) ;
#101119=VECTOR ( 'NONE', #86363, 999.9999999999998863 ) ;
#101121=DIRECTION ( 'NONE',  ( -0.7071067811865486830, -0.7071067811865464625, 0.000000000000000000 ) ) ;
#101122=EDGE_CURVE ( 'NONE', #94913, #120463, #140284, .T. ) ;
#101125=ADVANCED_FACE ( 'NONE', ( #119224 ), #53252, .F. ) ;
#101128=ORIENTED_EDGE ( 'NONE', *, *, #130389, .F. ) ;
#101129=EDGE_CURVE ( 'NONE', #68093, #119637, #57668, .T. ) ;
#101130=DIRECTION ( 'NONE',  ( 0.3543493200069162685, -0.000000000000000000, -0.9351131265310288487 ) ) ;
#101133=DIRECTION ( 'NONE',  ( 0.7071067811865487940, 0.7071067811865463515, -0.000000000000000000 ) ) ;
#101134=CARTESIAN_POINT ( 'NONE',  ( 34.92499999999998295, 22.22500000000000142, 4.500000000000000888 ) ) ;
#101135=DIRECTION ( 'NONE',  ( 0.7071067811865487940, 0.7071067811865463515, 0.000000000000000000 ) ) ;
#101136=ORIENTED_EDGE ( 'NONE', *, *, #8146, .T. ) ;
#101137=DIRECTION ( 'NONE',  ( -0.7071067811865486830, 0.7071067811865464625, 0.000000000000000000 ) ) ;
#101138=FACE_OUTER_BOUND ( 'NONE', #53777, .T. ) ;
#101139=DIRECTION ( 'NONE',  ( 0.7071067811865487940, 0.7071067811865463515, 0.000000000000000000 ) ) ;
#101141=ORIENTED_EDGE ( 'NONE', *, *, #91430, .F. ) ;
#101142=VECTOR ( 'NONE', #52348, 1000.000000000000000 ) ;
#101143=ORIENTED_EDGE ( 'NONE', *, *, #19330, .T. ) ;
#101145=ORIENTED_EDGE ( 'NONE', *, *, #6349, .F. ) ;
#101146=VECTOR ( 'NONE', #87990, 1000.000000000000114 ) ;
#101147=ADVANCED_FACE ( 'NONE', ( #88043 ), #76473, .T. ) ;
#101149=CARTESIAN_POINT ( 'NONE',  ( 6.183988606268994381, 28.73617430169791476, 5.000000000000000000 ) ) ;
#101150=DIRECTION ( 'NONE',  ( -0.7071067811865486830, 0.7071067811865464625, 0.000000000000000000 ) ) ;
#101152=FACE_OUTER_BOUND ( 'NONE', #139178, .T. ) ;
#101153=CARTESIAN_POINT ( 'NONE',  ( 5.204170427930421283E-15, -12.41253812416063163, 4.000000000000000000 ) ) ;
#101155=ORIENTED_EDGE ( 'NONE', *, *, #94664, .F. ) ;
#101156=DIRECTION ( 'NONE',  ( -0.000000000000000000, -0.3543493200069152693, 0.9351131265310292928 ) ) ;
#101158=ADVANCED_FACE ( 'NONE', ( #87336 ), #110478, .F. ) ;
#101159=ORIENTED_EDGE ( 'NONE', *, *, #30496, .F. ) ;
#101162=CARTESIAN_POINT ( 'NONE',  ( 17.51078643762690845, -27.52281430457043143, 5.000000000000000000 ) ) ;
#101165=FACE_BOUND ( 'NONE', #1807, .T. ) ;
#101166=DIRECTION ( 'NONE',  ( 0.3543493200069162685, -0.000000000000000000, -0.9351131265310288487 ) ) ;
#101167=EDGE_CURVE ( 'NONE', #27559, #48586, #75056, .T. ) ;
#101168=DIRECTION ( 'NONE',  ( 0.7071067811865486830, -0.7071067811865464625, -0.000000000000000000 ) ) ;
#101170=LINE ( 'NONE', #124362, #101272 ) ;
#101171=VECTOR ( 'NONE', #13253, 1000.000000000000000 ) ;
#101172=VECTOR ( 'NONE', #8754, 999.9999999999998863 ) ;
#101173=DIRECTION ( 'NONE',  ( 0.7071067811865487940, 0.7071067811865463515, 0.000000000000000000 ) ) ;
#101175=ORIENTED_EDGE ( 'NONE', *, *, #17605, .T. ) ;
#101177=EDGE_LOOP ( 'NONE', ( #89997, #25218, #97255, #40452 ) ) ;
#101179=ORIENTED_EDGE ( 'NONE', *, *, #93264, .F. ) ;
#101180=CARTESIAN_POINT ( 'NONE',  ( 20.81601139373100295, 28.73617430169773002, 5.000000000000000000 ) ) ;
#101184=CARTESIAN_POINT ( 'NONE',  ( -6.183988606268994381, 28.73617430169791476, 5.000000000000000000 ) ) ;
#101185=CARTESIAN_POINT ( 'NONE',  ( 34.92499999999998295, -22.22500000000000142, 4.500000000000000888 ) ) ;
#101186=FACE_OUTER_BOUND ( 'NONE', #111298, .T. ) ;
#101187=EDGE_CURVE ( 'NONE', #89674, #3009, #64159, .T. ) ;
#101189=DIRECTION ( 'NONE',  ( -0.3543493200069163240, -0.000000000000000000, 0.9351131265310288487 ) ) ;
#101190=DIRECTION ( 'NONE',  ( -0.000000000000000000, 0.000000000000000000, 1.000000000000000000 ) ) ;
#101191=CARTESIAN_POINT ( 'NONE',  ( -6.707106781186501721, 20.25929247661552424, 5.000000000000000000 ) ) ;
#101194=LINE ( 'NONE', #1832, #35850 ) ;
#101195=LINE ( 'NONE', #1833, #141094 ) ;
#101196=LINE ( 'NONE', #35974, #46811 ) ;
#101197=ORIENTED_EDGE ( 'NONE', *, *, #36450, .F. ) ;
#101198=CARTESIAN_POINT ( 'NONE',  ( -59.99451991528749772, 28.92564299267980132, 4.000000000000000000 ) ) ;
#101199=PLANE ( 'NONE',  #127540 ) ;
#101200=ORIENTED_EDGE ( 'NONE', *, *, #32301, .T. ) ;
#101201=ORIENTED_EDGE ( 'NONE', *, *, #22341, .T. ) ;
#101202=EDGE_CURVE ( 'NONE', #56149, #94083, #8990, .T. ) ;
#101203=VERTEX_POINT ( 'NONE', #11147 ) ;
#101205=AXIS2_PLACEMENT_3D ( 'NONE', #10967, #111003, #75561 ) ;
#101206=ORIENTED_EDGE ( 'NONE', *, *, #136392, .F. ) ;
#101208=VECTOR ( 'NONE', #3164, 1000.000000000000000 ) ;
#101211=LINE ( 'NONE', #69322, #140069 ) ;
#101212=ORIENTED_EDGE ( 'NONE', *, *, #15901, .T. ) ;
#101213=ORIENTED_EDGE ( 'NONE', *, *, #40780, .T. ) ;
#101214=CARTESIAN_POINT ( 'NONE',  ( -34.82816939922328459, 6.759292476615660128, 4.000000000000000000 ) ) ;
#101215=VECTOR ( 'NONE', #15018, 1000.000000000000000 ) ;
#101216=LINE ( 'NONE', #1858, #72563 ) ;
#101217=ORIENTED_EDGE ( 'NONE', *, *, #63195, .T. ) ;
#101220=DIRECTION ( 'NONE',  ( -0.000000000000000000, 0.3543493200069153248, 0.9351131265310292928 ) ) ;
#101221=FACE_OUTER_BOUND ( 'NONE', #14418, .T. ) ;
#101222=ORIENTED_EDGE ( 'NONE', *, *, #130086, .F. ) ;
#101223=LINE ( 'NONE', #113520, #71283 ) ;
#101224=VERTEX_POINT ( 'NONE', #120641 ) ;
#101225=VERTEX_POINT ( 'NONE', #21359 ) ;
#101226=ORIENTED_EDGE ( 'NONE', *, *, #101244, .T. ) ;
#101227=EDGE_CURVE ( 'NONE', #41056, #139347, #44582, .T. ) ;
#101229=AXIS2_PLACEMENT_3D ( 'NONE', #13554, #99877, #110717 ) ;
#101230=EDGE_CURVE ( 'NONE', #11497, #141976, #41679, .T. ) ;
#101232=DIRECTION ( 'NONE',  ( 0.6830127018922180770, -0.6830127018922204085, -0.2588190451025213501 ) ) ;
#101233=CARTESIAN_POINT ( 'NONE',  ( -36.29974487139159578, -27.71228299555231445, 4.000000000000000000 ) ) ;
#101234=EDGE_CURVE ( 'NONE', #36181, #74016, #54016, .T. ) ;
#101235=EDGE_CURVE ( 'NONE', #87818, #98610, #98212, .T. ) ;
#101236=ADVANCED_FACE ( 'NONE', ( #85892 ), #66307, .T. ) ;
#101237=CARTESIAN_POINT ( 'NONE',  ( -69.18398860626899705, 28.73617430169835529, 5.000000000000000000 ) ) ;
#101238=ORIENTED_EDGE ( 'NONE', *, *, #124096, .F. ) ;
#101239=PLANE ( 'NONE',  #107492 ) ;
#101240=EDGE_CURVE ( 'NONE', #90151, #118264, #19909, .T. ) ;
#101241=EDGE_CURVE ( 'NONE', #113850, #88227, #141722, .T. ) ;
#101243=DIRECTION ( 'NONE',  ( -0.7071067811865487940, 0.7071067811865463515, 0.000000000000000000 ) ) ;
#101244=EDGE_CURVE ( 'NONE', #118849, #121710, #42425, .T. ) ;
#101245=DIRECTION ( 'NONE',  ( 0.6830127018922180770, -0.6830127018922204085, -0.2588190451025213501 ) ) ;
#101248=ORIENTED_EDGE ( 'NONE', *, *, #30517, .F. ) ;
#101249=ORIENTED_EDGE ( 'NONE', *, *, #43851, .T. ) ;
#101251=ORIENTED_EDGE ( 'NONE', *, *, #85649, .T. ) ;
#101254=EDGE_CURVE ( 'NONE', #126555, #30495, #11883, .T. ) ;
#101255=LINE ( 'NONE', #33878, #47326 ) ;
#101256=LINE ( 'NONE', #37448, #4189 ) ;
#101257=CARTESIAN_POINT ( 'NONE',  ( 22.49999999999984013, -19.53360074219753884, 5.000000000000000000 ) ) ;
#101260=AXIS2_PLACEMENT_3D ( 'NONE', #2485, #38025, #115517 ) ;
#101263=CARTESIAN_POINT ( 'NONE',  ( 18.18398860626898994, 28.73617430169800002, 5.000000000000000000 ) ) ;
#101264=PLANE ( 'NONE',  #102013 ) ;
#101265=VERTEX_POINT ( 'NONE', #58326 ) ;
#101267=AXIS2_PLACEMENT_3D ( 'NONE', #122992, #134600, #135319 ) ;
#101268=EDGE_CURVE ( 'NONE', #122875, #81952, #102507, .T. ) ;
#101269=DIRECTION ( 'NONE',  ( -0.000000000000000000, 0.000000000000000000, 1.000000000000000000 ) ) ;
#101270=DIRECTION ( 'NONE',  ( -0.7071067811865486830, -0.7071067811865464625, 0.000000000000000000 ) ) ;
#101272=VECTOR ( 'NONE', #25756, 1000.000000000000000 ) ;
#101273=DIRECTION ( 'NONE',  ( -0.3543493200069162685, -0.000000000000000000, -0.9351131265310288487 ) ) ;
#101274=CARTESIAN_POINT ( 'NONE',  ( 9.183988606268997046, 28.73617430169793607, 5.000000000000000000 ) ) ;
#101275=ORIENTED_EDGE ( 'NONE', *, *, #110861, .T. ) ;
#101276=ORIENTED_EDGE ( 'NONE', *, *, #2911, .T. ) ;
#101277=DIRECTION ( 'NONE',  ( -0.000000000000000000, -0.3543493200069152693, 0.9351131265310292928 ) ) ;
#101278=ORIENTED_EDGE ( 'NONE', *, *, #47938, .F. ) ;
#101279=EDGE_CURVE ( 'NONE', #82336, #19260, #2425, .T. ) ;
#101280=AXIS2_PLACEMENT_3D ( 'NONE', #87647, #141307, #107933 ) ;
#101281=AXIS2_PLACEMENT_3D ( 'NONE', #85464, #41254, #138449 ) ;
#101283=AXIS2_PLACEMENT_3D ( 'NONE', #113249, #49479, #4428 ) ;
#101285=CARTESIAN_POINT ( 'NONE',  ( -5.999999999999956479, 9.631307414974321190, -9.079085613539556121 ) ) ;
#101286=DIRECTION ( 'NONE',  ( 0.7071067811865487940, 0.7071067811865463515, 0.000000000000000000 ) ) ;
#101288=DIRECTION ( 'NONE',  ( -0.6830127018922181881, 0.6830127018922202975, -0.2588190451025214056 ) ) ;
#101289=DIRECTION ( 'NONE',  ( -0.3543493200069162685, -0.000000000000000000, -0.9351131265310288487 ) ) ;
#101290=DIRECTION ( 'NONE',  ( -0.6830127018922180770, -0.6830127018922204085, -0.2588190451025213501 ) ) ;
#101292=DIRECTION ( 'NONE',  ( 1.000000000000000000, 0.000000000000000000, 0.000000000000000000 ) ) ;
#101293=VECTOR ( 'NONE', #74435, 1000.000000000000000 ) ;
#101294=LINE ( 'NONE', #104117, #83845 ) ;
#101295=CARTESIAN_POINT ( 'NONE',  ( -6.299744871391586898, -27.71228299555210484, 4.000000000000000000 ) ) ;
#101296=ORIENTED_EDGE ( 'NONE', *, *, #137788, .T. ) ;
#101297=CARTESIAN_POINT ( 'NONE',  ( -20.99999999999985079, -2.904428200921332248, -6.989807076074896486 ) ) ;
#101298=ADVANCED_FACE ( 'NONE', ( #81478 ), #45989, .F. ) ;
#101302=EDGE_CURVE ( 'NONE', #61052, #74659, #124236, .T. ) ;
#101303=PLANE ( 'NONE',  #101229 ) ;
#101307=ORIENTED_EDGE ( 'NONE', *, *, #130646, .F. ) ;
#101308=CARTESIAN_POINT ( 'NONE',  ( 54.18398860626899705, 28.73617430169825226, 5.000000000000000000 ) ) ;
#101309=LINE ( 'NONE', #81739, #113730 ) ;
#101310=ADVANCED_FACE ( 'NONE', ( #46738 ), #25625, .F. ) ;
#101311=CARTESIAN_POINT ( 'NONE',  ( -17.29298673570684386, -21.74070752338406720, 4.999753212805220670 ) ) ;
#101312=EDGE_LOOP ( 'NONE', ( #105767, #68090, #48430, #74372 ) ) ;
#101313=PLANE ( 'NONE',  #127254 ) ;
#101315=DIRECTION ( 'NONE',  ( 0.7071067811865487940, 0.7071067811865463515, 0.000000000000000000 ) ) ;
#101316=VERTEX_POINT ( 'NONE', #56171 ) ;
#101317=VECTOR ( 'NONE', #119220, 1000.000000000000000 ) ;
#101318=CARTESIAN_POINT ( 'NONE',  ( 29.29289321881325137, -6.740707523384214639, 5.000000000000000000 ) ) ;
#101319=CARTESIAN_POINT ( 'NONE',  ( -12.48921356237309155, -27.52281430457064104, 5.000000000000000000 ) ) ;
#101320=LINE ( 'NONE', #79633, #73383 ) ;
#101321=CARTESIAN_POINT ( 'NONE',  ( 33.48921356237309510, -27.52281430457078670, 5.000000000000000000 ) ) ;
#101323=VERTEX_POINT ( 'NONE', #67008 ) ;
#101324=ORIENTED_EDGE ( 'NONE', *, *, #95731, .F. ) ;
#101326=ORIENTED_EDGE ( 'NONE', *, *, #106127, .F. ) ;
#101327=EDGE_CURVE ( 'NONE', #108649, #99762, #69901, .T. ) ;
#101328=LINE ( 'NONE', #79643, #37035 ) ;
#101329=DIRECTION ( 'NONE',  ( 0.7071067811865486830, -0.7071067811865464625, -0.000000000000000000 ) ) ;
#101330=PLANE ( 'NONE',  #68935 ) ;
#101331=CARTESIAN_POINT ( 'NONE',  ( 31.49999999999978684, -14.94781430457067906, 5.000000000000000000 ) ) ;
#101332=ORIENTED_EDGE ( 'NONE', *, *, #70716, .T. ) ;
#101333=CARTESIAN_POINT ( 'NONE',  ( 17.51078643762690845, -27.52281430457043143, 5.000000000000000000 ) ) ;
#101334=LINE ( 'NONE', #133965, #116043 ) ;
#101335=CARTESIAN_POINT ( 'NONE',  ( -7.499999999999952927, 3.431123077392153053, 4.000000000000000000 ) ) ;
#101337=VERTEX_POINT ( 'NONE', #57580 ) ;
#101338=EDGE_CURVE ( 'NONE', #75799, #106925, #47447, .T. ) ;
#101339=DIRECTION ( 'NONE',  ( -0.7071067811865486830, -0.7071067811865464625, 0.000000000000000000 ) ) ;
#101340=DIRECTION ( 'NONE',  ( -0.000000000000000000, 0.000000000000000000, 1.000000000000000000 ) ) ;
#101342=ORIENTED_EDGE ( 'NONE', *, *, #7475, .T. ) ;
#101343=EDGE_CURVE ( 'NONE', #128314, #32532, #135148, .T. ) ;
#101344=PLANE ( 'NONE',  #102509 ) ;
#101349=CARTESIAN_POINT ( 'NONE',  ( -13.10332671766740020, 3.690788593506699300, 4.000000000000000000 ) ) ;
#101350=CARTESIAN_POINT ( 'NONE',  ( 8.994519915287490619, 28.92564299267944250, 4.000000000000000000 ) ) ;
#101352=ADVANCED_FACE ( 'NONE', ( #100354 ), #23489, .F. ) ;
#101353=EDGE_LOOP ( 'NONE', ( #102235, #42973, #63783, #48006 ) ) ;
#101354=ORIENTED_EDGE ( 'NONE', *, *, #89221, .F. ) ;
#101355=CARTESIAN_POINT ( 'NONE',  ( -21.18398860626899349, 28.73617430169802134, 5.000000000000000000 ) ) ;
#101356=ORIENTED_EDGE ( 'NONE', *, *, #110861, .F. ) ;
#101357=ORIENTED_EDGE ( 'NONE', *, *, #116657, .F. ) ;
#101358=EDGE_CURVE ( 'NONE', #7759, #68447, #1005, .T. ) ;
#101359=AXIS2_PLACEMENT_3D ( 'NONE', #122689, #132899, #56055 ) ;
#101360=CARTESIAN_POINT ( 'NONE',  ( 8.292893218813404133, 2.259292476615696099, 5.000000000000000000 ) ) ;
#101361=EDGE_CURVE ( 'NONE', #61121, #39262, #35842, .T. ) ;
#101362=ORIENTED_EDGE ( 'NONE', *, *, #99012, .T. ) ;
#101364=FACE_OUTER_BOUND ( 'NONE', #88642, .T. ) ;
#101365=DIRECTION ( 'NONE',  ( 0.7071067811865487940, 0.7071067811865463515, 0.000000000000000000 ) ) ;
#101366=AXIS2_PLACEMENT_3D ( 'NONE', #29365, #76481, #108326 ) ;
#101367=DIRECTION ( 'NONE',  ( -0.7071067811865487940, 0.7071067811865463515, 0.000000000000000000 ) ) ;
#101368=ORIENTED_EDGE ( 'NONE', *, *, #41328, .T. ) ;
#101369=CARTESIAN_POINT ( 'NONE',  ( -2.999999999999981792, -13.39766691384884290, -10.96608748226465124 ) ) ;
#101371=ORIENTED_EDGE ( 'NONE', *, *, #112062, .T. ) ;
#101373=ORIENTED_EDGE ( 'NONE', *, *, #60001, .F. ) ;
#101374=LINE ( 'NONE', #46330, #9759 ) ;
#101375=ADVANCED_FACE ( 'NONE', ( #59036 ), #67759, .F. ) ;
#101376=ORIENTED_EDGE ( 'NONE', *, *, #105684, .T. ) ;
#101377=PLANE ( 'NONE',  #25001 ) ;
#101378=ORIENTED_EDGE ( 'NONE', *, *, #110774, .T. ) ;
#101379=ORIENTED_EDGE ( 'NONE', *, *, #119556, .F. ) ;
#101380=VECTOR ( 'NONE', #108471, 1000.000000000000227 ) ;
#101381=ORIENTED_EDGE ( 'NONE', *, *, #110002, .T. ) ;
#101382=VECTOR ( 'NONE', #89418, 1000.000000000000000 ) ;
#101384=LINE ( 'NONE', #25246, #140126 ) ;
#101386=CARTESIAN_POINT ( 'NONE',  ( 11.81601139373100651, 28.73617430169779041, 5.000000000000000000 ) ) ;
#101388=FACE_OUTER_BOUND ( 'NONE', #17732, .T. ) ;
#101389=DIRECTION ( 'NONE',  ( 0.000000000000000000, -1.000000000000000000, 0.000000000000000000 ) ) ;
#101390=DIRECTION ( 'NONE',  ( -0.7071067811865486830, 0.7071067811865464625, 0.000000000000000000 ) ) ;
#101391=DIRECTION ( 'NONE',  ( 0.3543493200069162685, -0.000000000000000000, -0.9351131265310288487 ) ) ;
#101393=LINE ( 'NONE', #99225, #71415 ) ;
#101394=VERTEX_POINT ( 'NONE', #103188 ) ;
#101395=CARTESIAN_POINT ( 'NONE',  ( 51.18398860626899705, 28.73617430169823095, 5.000000000000000000 ) ) ;
#101396=PLANE ( 'NONE',  #118932 ) ;
#101397=ORIENTED_EDGE ( 'NONE', *, *, #58516, .F. ) ;
#101399=CARTESIAN_POINT ( 'NONE',  ( 48.29974487139158867, -27.71228299555239971, 4.000000000000000000 ) ) ;
#101400=ORIENTED_EDGE ( 'NONE', *, *, #85839, .F. ) ;
#101401=VECTOR ( 'NONE', #90349, 1000.000000000000227 ) ;
#101402=FACE_OUTER_BOUND ( 'NONE', #69937, .T. ) ;
#101404=LINE ( 'NONE', #25267, #16155 ) ;
#101406=EDGE_LOOP ( 'NONE', ( #123459, #90020, #43652, #60434 ) ) ;
#101407=CARTESIAN_POINT ( 'NONE',  ( 25.01899999999999835, 3.174999999999997158, 4.000000000000000000 ) ) ;
#101408=EDGE_LOOP ( 'NONE', ( #141438, #125731, #138762, #15393 ) ) ;
#101409=( BOUNDED_CURVE ( )  B_SPLINE_CURVE ( 3, ( #125793, #92412, #56985, #70013 ),
 .UNSPECIFIED., .F., .T. ) 
 B_SPLINE_CURVE_WITH_KNOTS ( ( 4, 4 ),
 ( 5.143245962375958769, 6.645403452391243526 ),
 .UNSPECIFIED. ) 
 CURVE ( )  GEOMETRIC_REPRESENTATION_ITEM ( )  RATIONAL_B_SPLINE_CURVE ( ( 1.000000000000000000, 0.8206354192515232793, 0.8206354192515232793, 1.000000000000000000 ) ) 
 REPRESENTATION_ITEM ( '' )  );
#101410=CARTESIAN_POINT ( 'NONE',  ( -57.48921356237308800, -27.52281430457095368, 5.000000000000000000 ) ) ;
#101411=EDGE_CURVE ( 'NONE', #80458, #114963, #80060, .T. ) ;
#101413=EDGE_LOOP ( 'NONE', ( #31376, #40265, #34021, #80970 ) ) ;
#101417=CARTESIAN_POINT ( 'NONE',  ( -34.47516574401891631, -5.971932658884116840, 4.998110765256836174 ) ) ;
#101418=ORIENTED_EDGE ( 'NONE', *, *, #114167, .F. ) ;
#101419=ORIENTED_EDGE ( 'NONE', *, *, #10478, .T. ) ;
#101420=EDGE_CURVE ( 'NONE', #40729, #16613, #93753, .T. ) ;
#101423=DIRECTION ( 'NONE',  ( -0.000000000000000000, 0.000000000000000000, 1.000000000000000000 ) ) ;
#101424=LINE ( 'NONE', #10134, #46547 ) ;
#101425=LINE ( 'NONE', #26721, #91389 ) ;
#101426=VECTOR ( 'NONE', #30065, 1000.000000000000000 ) ;
#101428=DIRECTION ( 'NONE',  ( -0.7071067811865487940, 0.7071067811865463515, 0.000000000000000000 ) ) ;
#101430=AXIS2_PLACEMENT_3D ( 'NONE', #91802, #115664, #36707 ) ;
#101431=ADVANCED_FACE ( 'NONE', ( #48835 ), #70617, .T. ) ;
#101434=ORIENTED_EDGE ( 'NONE', *, *, #92127, .T. ) ;
#101435=CARTESIAN_POINT ( 'NONE',  ( 25.49999999999983302, 19.46639925780206326, 5.000000000000000000 ) ) ;
#101436=ORIENTED_EDGE ( 'NONE', *, *, #825, .T. ) ;
#101438=VERTEX_POINT ( 'NONE', #105329 ) ;
#101440=EDGE_CURVE ( 'NONE', #143191, #20063, #15431, .T. ) ;
#101442=CARTESIAN_POINT ( 'NONE',  ( -54.48921356237310221, -27.52281430457093236, 5.000000000000000000 ) ) ;
#101444=DIRECTION ( 'NONE',  ( -0.7071067811865486830, 0.7071067811865464625, 0.000000000000000000 ) ) ;
#101445=ORIENTED_EDGE ( 'NONE', *, *, #17173, .T. ) ;
#101446=EDGE_CURVE ( 'NONE', #86990, #111757, #104620, .T. ) ;
#101447=CARTESIAN_POINT ( 'NONE',  ( 27.85005128541007124, -8.240707523384196875, 17.25253755692245861 ) ) ;
#101449=LINE ( 'NONE', #2097, #2195 ) ;
#101450=AXIS2_PLACEMENT_3D ( 'NONE', #63959, #43613, #20416 ) ;
#101451=CARTESIAN_POINT ( 'NONE',  ( 18.79289321881332597, -5.240707523384228850, 5.000000000000000000 ) ) ;
#101452=PLANE ( 'NONE',  #92918 ) ;
#101453=FACE_OUTER_BOUND ( 'NONE', #14002, .T. ) ;
#101454=LINE ( 'NONE', #126086, #5414 ) ;
#101455=CARTESIAN_POINT ( 'NONE',  ( -31.82816939922330945, 6.759292476615653023, 4.000000000000000000 ) ) ;
#101457=CARTESIAN_POINT ( 'NONE',  ( 22.17183060077632106, -5.240707523384228850, 4.000000000000000000 ) ) ;
#101458=LINE ( 'NONE', #135542, #1904 ) ;
#101459=DIRECTION ( 'NONE',  ( 0.6830127018922180770, -0.6830127018922204085, -0.2588190451025213501 ) ) ;
#101460=DIRECTION ( 'NONE',  ( 0.7071067811865487940, 0.7071067811865463515, 0.000000000000000000 ) ) ;
#101461=EDGE_LOOP ( 'NONE', ( #74520, #52288, #3199 ) ) ;
#101462=ORIENTED_EDGE ( 'NONE', *, *, #28259, .T. ) ;
#101464=ORIENTED_EDGE ( 'NONE', *, *, #140070, .T. ) ;
#101465=EDGE_LOOP ( 'NONE', ( #21622, #66216, #30449, #30458 ) ) ;
#101466=ORIENTED_EDGE ( 'NONE', *, *, #138594, .T. ) ;
#101467=EDGE_CURVE ( 'NONE', #73986, #540, #137265, .T. ) ;
#101468=CARTESIAN_POINT ( 'NONE',  ( -30.65671000166194915, 3.759292476615681888, 13.27625715073258661 ) ) ;
#101469=CARTESIAN_POINT ( 'NONE',  ( -0.2997448713915885632, -27.71228299555206220, 4.000000000000000000 ) ) ;
#101470=DIRECTION ( 'NONE',  ( 0.7071067811865486830, -0.7071067811865464625, -0.000000000000000000 ) ) ;
#101471=VERTEX_POINT ( 'NONE', #82891 ) ;
#101474=LINE ( 'NONE', #56606, #41695 ) ;
#101475=DIRECTION ( 'NONE',  ( 0.6830127018922180770, -0.6830127018922204085, -0.2588190451025213501 ) ) ;
#101476=VECTOR ( 'NONE', #99746, 1000.000000000000227 ) ;
#101477=CARTESIAN_POINT ( 'NONE',  ( 18.48921356237309510, -27.52281430457068367, 5.000000000000000000 ) ) ;
#101478=CARTESIAN_POINT ( 'NONE',  ( -14.29387692260794118, 22.22500000000000142, 4.000000000000000000 ) ) ;
#101479=CARTESIAN_POINT ( 'NONE',  ( 19.35292824042819149, -2.786763769301527027, 4.186878071398587586 ) ) ;
#101480=PLANE ( 'NONE',  #98007 ) ;
#101481=LINE ( 'NONE', #2134, #88450 ) ;
#101482=AXIS2_PLACEMENT_3D ( 'NONE', #44185, #87671, #42044 ) ;
#101483=DIRECTION ( 'NONE',  ( -0.7071067811865487940, 0.7071067811865463515, 0.000000000000000000 ) ) ;
#101484=CARTESIAN_POINT ( 'NONE',  ( 16.49999999999987566, 1.030536316426515553, -5.498701923753840148 ) ) ;
#101485=LINE ( 'NONE', #24640, #70899 ) ;
#101486=VECTOR ( 'NONE', #131156, 1000.000000000000000 ) ;
#101487=CARTESIAN_POINT ( 'NONE',  ( -21.70710678118639692, -15.74070752338412049, 5.000000000000000000 ) ) ;
#101488=ADVANCED_FACE ( 'NONE', ( #127080 ), #59719, .F. ) ;
#101489=LINE ( 'NONE', #21066, #107074 ) ;
#101491=ORIENTED_EDGE ( 'NONE', *, *, #53829, .T. ) ;
#101493=EDGE_LOOP ( 'NONE', ( #12243, #71662, #15368, #28552 ) ) ;
#101494=EDGE_CURVE ( 'NONE', #3971, #108000, #127827, .T. ) ;
#101495=DIRECTION ( 'NONE',  ( -0.6830127018922180770, -0.6830127018922204085, -0.2588190451025213501 ) ) ;
#101497=CARTESIAN_POINT ( 'NONE',  ( 84.18398860626899705, 28.73617430169846187, 5.000000000000000000 ) ) ;
#101499=VECTOR ( 'NONE', #86138, 999.9999999999998863 ) ;
#101501=ORIENTED_EDGE ( 'NONE', *, *, #71896, .F. ) ;
#101502=EDGE_CURVE ( 'NONE', #119845, #53035, #38662, .T. ) ;
#101503=ORIENTED_EDGE ( 'NONE', *, *, #116656, .T. ) ;
#101504=CARTESIAN_POINT ( 'NONE',  ( -45.18398860626900415, 28.73617430169818832, 5.000000000000000000 ) ) ;
#101505=VECTOR ( 'NONE', #39065, 1000.000000000000227 ) ;
#101506=CARTESIAN_POINT ( 'NONE',  ( 0.000000000000000000, 0.000000000000000000, 5.000000000000000000 ) ) ;
#101507=VECTOR ( 'NONE', #85742, 1000.000000000000000 ) ;
#101508=VECTOR ( 'NONE', #90537, 1000.000000000000000 ) ;
#101509=VERTEX_POINT ( 'NONE', #73439 ) ;
#101510=EDGE_LOOP ( 'NONE', ( #50497, #82043, #20783, #94091 ) ) ;
#101511=EDGE_CURVE ( 'NONE', #24720, #19355, #6690, .T. ) ;
#101512=ORIENTED_EDGE ( 'NONE', *, *, #11243, .F. ) ;
#101514=EDGE_CURVE ( 'NONE', #60374, #21741, #40805, .T. ) ;
#101517=ORIENTED_EDGE ( 'NONE', *, *, #45307, .T. ) ;
#101519=VERTEX_POINT ( 'NONE', #71303 ) ;
#101520=VERTEX_POINT ( 'NONE', #115458 ) ;
#101521=ORIENTED_EDGE ( 'NONE', *, *, #117436, .F. ) ;
#101522=VECTOR ( 'NONE', #64726, 1000.000000000000000 ) ;
#101523=PLANE ( 'NONE',  #49485 ) ;
#101525=LINE ( 'NONE', #124014, #111301 ) ;
#101526=EDGE_CURVE ( 'NONE', #40992, #96671, #27772, .T. ) ;
#101527=EDGE_LOOP ( 'NONE', ( #81741, #127802, #71722, #79815 ) ) ;
#101528=DIRECTION ( 'NONE',  ( 1.000000000000000000, 0.000000000000000000, 0.000000000000000000 ) ) ;
#101530=DIRECTION ( 'NONE',  ( -0.7071067811865486830, -0.7071067811865464625, 0.000000000000000000 ) ) ;
#101531=ADVANCED_FACE ( 'NONE', ( #94449 ), #72769, .F. ) ;
#101532=FACE_BOUND ( 'NONE', #80718, .T. ) ;
#101533=ORIENTED_EDGE ( 'NONE', *, *, #83599, .T. ) ;
#101534=DIRECTION ( 'NONE',  ( -0.3543493200069162685, -0.000000000000000000, -0.9351131265310288487 ) ) ;
#101537=DIRECTION ( 'NONE',  ( 0.7071067811865487940, -0.7071067811865463515, 0.000000000000000000 ) ) ;
#101538=EDGE_CURVE ( 'NONE', #101635, #130156, #106019, .T. ) ;
#101540=CYLINDRICAL_SURFACE ( 'NONE', #57432, 0.5000000000000004441 ) ;
#101542=VERTEX_POINT ( 'NONE', #139435 ) ;
#101545=ORIENTED_EDGE ( 'NONE', *, *, #88197, .F. ) ;
#101546=DIRECTION ( 'NONE',  ( 0.7071067811865487940, 0.7071067811865463515, 0.000000000000000000 ) ) ;
#101548=VERTEX_POINT ( 'NONE', #84334 ) ;
#101550=CARTESIAN_POINT ( 'NONE',  ( -27.00548008471251293, 28.92564299267919381, 4.000000000000000000 ) ) ;
#101551=EDGE_CURVE ( 'NONE', #20167, #34213, #7427, .T. ) ;
#101553=DIRECTION ( 'NONE',  ( -0.000000000000000000, 0.3543493200069153248, 0.9351131265310292928 ) ) ;
#101554=DIRECTION ( 'NONE',  ( -0.000000000000000000, 0.000000000000000000, 1.000000000000000000 ) ) ;
#101560=DIRECTION ( 'NONE',  ( -0.7071067811865487940, 0.7071067811865463515, -0.000000000000000000 ) ) ;
#101561=VECTOR ( 'NONE', #125992, 1000.000000000000114 ) ;
#101563=VERTEX_POINT ( 'NONE', #31358 ) ;
#101564=VECTOR ( 'NONE', #92791, 1000.000000000000227 ) ;
#101565=VECTOR ( 'NONE', #84786, 1000.000000000000000 ) ;
#101568=CARTESIAN_POINT ( 'NONE',  ( 32.20710678118632586, -5.240707523384230626, 5.000000000000000000 ) ) ;
#101569=VERTEX_POINT ( 'NONE', #75578 ) ;
#101570=FACE_OUTER_BOUND ( 'NONE', #8303, .T. ) ;
#101572=VECTOR ( 'NONE', #2458, 1000.000000000000000 ) ;
#101573=LINE ( 'NONE', #134232, #44472 ) ;
#101575=EDGE_CURVE ( 'NONE', #123357, #88687, #19412, .T. ) ;
#101576=DIRECTION ( 'NONE',  ( 0.7071067811865487940, -0.7071067811865463515, 0.000000000000000000 ) ) ;
#101579=DIRECTION ( 'NONE',  ( -0.7071067811865486830, -0.7071067811865464625, 0.000000000000000000 ) ) ;
#101580=EDGE_CURVE ( 'NONE', #111310, #305, #8471, .T. ) ;
#101581=FACE_OUTER_BOUND ( 'NONE', #48975, .T. ) ;
#101583=ORIENTED_EDGE ( 'NONE', *, *, #43215, .F. ) ;
#101585=PLANE ( 'NONE',  #130590 ) ;
#101586=ORIENTED_EDGE ( 'NONE', *, *, #121714, .T. ) ;
#101587=AXIS2_PLACEMENT_3D ( 'NONE', #69570, #61551, #15127 ) ;
#101588=LINE ( 'NONE', #100882, #74060 ) ;
#101589=EDGE_LOOP ( 'NONE', ( #130985, #99451, #42835, #131845 ) ) ;
#101592=PLANE ( 'NONE',  #91034 ) ;
#101594=EDGE_CURVE ( 'NONE', #23245, #27314, #65437, .T. ) ;
#101596=ORIENTED_EDGE ( 'NONE', *, *, #15388, .T. ) ;
#101597=CARTESIAN_POINT ( 'NONE',  ( -34.42500000000001137, -22.22500000000000142, 5.000000000000000000 ) ) ;
#101599=CARTESIAN_POINT ( 'NONE',  ( -21.48921356237309155, -27.52281430457070499, 5.000000000000000000 ) ) ;
#101600=DIRECTION ( 'NONE',  ( -0.6830127018922180770, -0.6830127018922204085, -0.2588190451025213501 ) ) ;
#101603=LINE ( 'NONE', #124087, #100217 ) ;
#101604=CIRCLE ( 'NONE', #129337, 5.968999999999998529 ) ;
#101605=ORIENTED_EDGE ( 'NONE', *, *, #27130, .T. ) ;
#101606=VECTOR ( 'NONE', #57792, 1000.000000000000000 ) ;
#101607=EDGE_CURVE ( 'NONE', #37108, #113729, #97273, .T. ) ;
#101608=DIRECTION ( 'NONE',  ( -0.000000000000000000, -0.3543493200069152693, 0.9351131265310292928 ) ) ;
#101609=CARTESIAN_POINT ( 'NONE',  ( -24.29974487139158867, -27.71228299555223273, 4.000000000000000000 ) ) ;
#101610=ORIENTED_EDGE ( 'NONE', *, *, #80022, .T. ) ;
#101611=EDGE_CURVE ( 'NONE', #54692, #44739, #142274, .T. ) ;
#101612=ORIENTED_EDGE ( 'NONE', *, *, #131219, .F. ) ;
#101615=DIRECTION ( 'NONE',  ( 1.000000000000000000, 0.000000000000000000, 0.000000000000000000 ) ) ;
#101616=ORIENTED_EDGE ( 'NONE', *, *, #88700, .F. ) ;
#101617=VECTOR ( 'NONE', #9335, 1000.000000000000000 ) ;
#101618=ADVANCED_FACE ( 'NONE', ( #53078 ), #142957, .F. ) ;
#101619=LINE ( 'NONE', #71686, #34459 ) ;
#101621=ORIENTED_EDGE ( 'NONE', *, *, #120441, .T. ) ;
#101622=CARTESIAN_POINT ( 'NONE',  ( 0.000000000000000000, 0.000000000000000000, 5.000000000000000000 ) ) ;
#101623=CARTESIAN_POINT ( 'NONE',  ( 12.29974487139158512, -27.71228299555214747, 4.000000000000000000 ) ) ;
#101625=EDGE_CURVE ( 'NONE', #118545, #101563, #29903, .T. ) ;
#101626=VECTOR ( 'NONE', #37984, 1000.000000000000000 ) ;
#101627=LINE ( 'NONE', #13879, #81796 ) ;
#101628=DIRECTION ( 'NONE',  ( 1.000000000000000000, 0.000000000000000000, 0.000000000000000000 ) ) ;
#101629=DIRECTION ( 'NONE',  ( -0.3543493200069162685, -0.000000000000000000, -0.9351131265310288487 ) ) ;
#101631=ORIENTED_EDGE ( 'NONE', *, *, #5607, .T. ) ;
#101632=VERTEX_POINT ( 'NONE', #20447 ) ;
#101634=ORIENTED_EDGE ( 'NONE', *, *, #126914, .F. ) ;
#101635=VERTEX_POINT ( 'NONE', #87155 ) ;
#101639=CARTESIAN_POINT ( 'NONE',  ( -34.49999999999976552, -2.173586137069173585, -4.605770156576189045 ) ) ;
#101640=EDGE_LOOP ( 'NONE', ( #119998, #58901, #123614, #140910, #108122 ) ) ;
#101641=DIRECTION ( 'NONE',  ( 0.7071067811865486830, -0.7071067811865464625, -0.000000000000000000 ) ) ;
#101643=CARTESIAN_POINT ( 'NONE',  ( -17.29289321881333308, -9.740707523384182664, 5.000000000000000000 ) ) ;
#101644=CARTESIAN_POINT ( 'NONE',  ( -81.48921356237309510, -27.52281430457112066, 5.000000000000000000 ) ) ;
#101646=ORIENTED_EDGE ( 'NONE', *, *, #67017, .T. ) ;
#101647=EDGE_CURVE ( 'NONE', #49817, #137771, #118338, .T. ) ;
#101648=CARTESIAN_POINT ( 'NONE',  ( -54.48921356237310221, -27.52281430457093236, 5.000000000000000000 ) ) ;
#101651=CARTESIAN_POINT ( 'NONE',  ( -16.49999999999987566, 19.46639925780206326, 5.000000000000000000 ) ) ;
#101653=FACE_OUTER_BOUND ( 'NONE', #8559, .T. ) ;
#101654=LINE ( 'NONE', #81370, #40010 ) ;
#101655=LINE ( 'NONE', #2313, #69003 ) ;
#101657=EDGE_CURVE ( 'NONE', #140051, #94242, #63304, .T. ) ;
#101658=LINE ( 'NONE', #35008, #102356 ) ;
#101660=ORIENTED_EDGE ( 'NONE', *, *, #84426, .F. ) ;
#101661=EDGE_LOOP ( 'NONE', ( #138998, #7009, #74307, #47754 ) ) ;
#101663=ORIENTED_EDGE ( 'NONE', *, *, #82165, .T. ) ;
#101664=CARTESIAN_POINT ( 'NONE',  ( -34.45011844616455221, -10.48371918836241257, 5.000000000000000888 ) ) ;
#101665=EDGE_LOOP ( 'NONE', ( #134417, #136299, #100435 ) ) ;
#101666=DIRECTION ( 'NONE',  ( 0.7071067811865487940, -0.7071067811865463515, 0.000000000000000000 ) ) ;
#101667=PLANE ( 'NONE',  #19084 ) ;
#101670=EDGE_CURVE ( 'NONE', #81264, #110646, #107473, .T. ) ;
#101671=DIRECTION ( 'NONE',  ( -0.7071067811865486830, -0.7071067811865464625, -0.000000000000000000 ) ) ;
#101673=ORIENTED_EDGE ( 'NONE', *, *, #56461, .T. ) ;
#101674=LINE ( 'NONE', #111860, #61293 ) ;
#101677=VECTOR ( 'NONE', #55522, 1000.000000000000000 ) ;
#101679=CARTESIAN_POINT ( 'NONE',  ( -25.49999999999982236, 10.46639925780215563, 5.000000000000000000 ) ) ;
#101680=( BOUNDED_CURVE ( )  B_SPLINE_CURVE ( 3, ( #42071, #109444, #53654, #65259 ),
 .UNSPECIFIED., .F., .F. ) 
 B_SPLINE_CURVE_WITH_KNOTS ( ( 4, 4 ),
 ( 5.043186909253406291, 5.074607125596344304 ),
 .UNSPECIFIED. ) 
 CURVE ( )  GEOMETRIC_REPRESENTATION_ITEM ( )  RATIONAL_B_SPLINE_CURVE ( ( 1.000000000000000000, 0.9999177325257868620, 0.9999177325257868620, 1.000000000000000000 ) ) 
 REPRESENTATION_ITEM ( '' )  );
#101683=ORIENTED_EDGE ( 'NONE', *, *, #7484, .F. ) ;
#101684=LINE ( 'NONE', #79279, #134534 ) ;
#101685=EDGE_CURVE ( 'NONE', #60588, #107292, #54551, .T. ) ;
#101686=ORIENTED_EDGE ( 'NONE', *, *, #98453, .F. ) ;
#101687=CARTESIAN_POINT ( 'NONE',  ( 0.000000000000000000, 0.000000000000000000, 5.000000000000000000 ) ) ;
#101688=DIRECTION ( 'NONE',  ( 0.7071067811865487940, 0.7071067811865463515, 0.000000000000000000 ) ) ;
#101689=DIRECTION ( 'NONE',  ( -0.7071067811865486830, -0.7071067811865464625, -0.000000000000000000 ) ) ;
#101690=DIRECTION ( 'NONE',  ( -0.7071067811865486830, 0.7071067811865464625, 0.000000000000000000 ) ) ;
#101692=VECTOR ( 'NONE', #113200, 1000.000000000000000 ) ;
#101696=ADVANCED_FACE ( 'NONE', ( #108154 ), #108869, .F. ) ;
#101697=DIRECTION ( 'NONE',  ( 4.681814790819592407E-17, 0.3543493200069153248, 0.9351131265310292928 ) ) ;
#101698=DIRECTION ( 'NONE',  ( 1.000000000000000000, 0.000000000000000000, 0.000000000000000000 ) ) ;
#101699=ORIENTED_EDGE ( 'NONE', *, *, #71492, .T. ) ;
#101700=ORIENTED_EDGE ( 'NONE', *, *, #93971, .F. ) ;
#101701=VECTOR ( 'NONE', #103399, 1000.000000000000000 ) ;
#101703=PLANE ( 'NONE',  #74742 ) ;
#101704=ORIENTED_EDGE ( 'NONE', *, *, #70586, .F. ) ;
#101707=EDGE_CURVE ( 'NONE', #87888, #69646, #32062, .T. ) ;
#101708=VERTEX_POINT ( 'NONE', #120450 ) ;
#101709=DIRECTION ( 'NONE',  ( 0.3543493200069162685, -0.000000000000000000, -0.9351131265310288487 ) ) ;
#101710=CARTESIAN_POINT ( 'NONE',  ( 28.49999999999980815, -2.568876922607781221, 4.000000000000000000 ) ) ;
#101711=CARTESIAN_POINT ( 'NONE',  ( 17.29298673570682254, -21.74070752338406720, 4.999753212805220670 ) ) ;
#101712=VECTOR ( 'NONE', #117538, 999.9999999999998863 ) ;
#101713=VECTOR ( 'NONE', #24949, 1000.000000000000000 ) ;
#101715=VECTOR ( 'NONE', #26220, 1000.000000000000000 ) ;
#101716=EDGE_CURVE ( 'NONE', #64740, #122408, #87869, .T. ) ;
#101717=FACE_BOUND ( 'NONE', #75760, .T. ) ;
#101718=CARTESIAN_POINT ( 'NONE',  ( 63.18398860626900415, 28.73617430169831621, 5.000000000000000000 ) ) ;
#101720=EDGE_CURVE ( 'NONE', #103883, #24621, #77024, .T. ) ;
#101721=LINE ( 'NONE', #98852, #115105 ) ;
#101722=DIRECTION ( 'NONE',  ( -0.7071067811865486830, -0.7071067811865464625, -0.000000000000000000 ) ) ;
#101723=ORIENTED_EDGE ( 'NONE', *, *, #142549, .F. ) ;
#101724=VECTOR ( 'NONE', #125190, 1000.000000000000227 ) ;
#101727=DIRECTION ( 'NONE',  ( 0.7071067811865487940, 0.7071067811865463515, 0.000000000000000000 ) ) ;
#101728=EDGE_LOOP ( 'NONE', ( #24767, #113907, #34170, #107407 ) ) ;
#101729=EDGE_LOOP ( 'NONE', ( #56696, #110886, #12840 ) ) ;
#101731=ORIENTED_EDGE ( 'NONE', *, *, #117008, .T. ) ;
#101732=EDGE_CURVE ( 'NONE', #85633, #4933, #33521, .T. ) ;
#101733=CARTESIAN_POINT ( 'NONE',  ( -10.06996025486402502, -0.7407075233842770334, 13.87443053587613129 ) ) ;
#101734=VERTEX_POINT ( 'NONE', #2987 ) ;
#101735=CARTESIAN_POINT ( 'NONE',  ( 12.48921356237309155, -27.52281430457064104, 5.000000000000000000 ) ) ;
#101737=EDGE_CURVE ( 'NONE', #72846, #126683, #113170, .T. ) ;
#101738=DIRECTION ( 'NONE',  ( -0.3543493200069163240, -0.000000000000000000, 0.9351131265310288487 ) ) ;
#101740=DIRECTION ( 'NONE',  ( 0.7071067811865486830, -0.7071067811865464625, -0.000000000000000000 ) ) ;
#101742=CARTESIAN_POINT ( 'NONE',  ( -27.18398860626900060, 28.73617430169806042, 5.000000000000000000 ) ) ;
#101743=LINE ( 'NONE', #33661, #9959 ) ;
#101746=EDGE_CURVE ( 'NONE', #87121, #27504, #137511, .T. ) ;
#101747=ORIENTED_EDGE ( 'NONE', *, *, #104535, .T. ) ;
#101748=CARTESIAN_POINT ( 'NONE',  ( -18.51789069628991768, -2.771357050275779610, 4.325358181756085330 ) ) ;
#101749=PLANE ( 'NONE',  #14211 ) ;
#101750=VERTEX_POINT ( 'NONE', #122627 ) ;
#101751=ORIENTED_EDGE ( 'NONE', *, *, #135297, .F. ) ;
#101754=ORIENTED_EDGE ( 'NONE', *, *, #106639, .T. ) ;
#101755=PLANE ( 'NONE',  #69484 ) ;
#101756=DIRECTION ( 'NONE',  ( 0.7071067811865486830, -0.7071067811865464625, -0.000000000000000000 ) ) ;
#101760=DIRECTION ( 'NONE',  ( 0.7071067811865487940, 0.7071067811865463515, -0.000000000000000000 ) ) ;
#101761=EDGE_CURVE ( 'NONE', #13547, #87703, #133524, .T. ) ;
#101762=CARTESIAN_POINT ( 'NONE',  ( -57.29974487139158157, -27.71228299555246011, 4.000000000000000000 ) ) ;
#101763=DIRECTION ( 'NONE',  ( -1.000000000000000000, 0.000000000000000000, -0.000000000000000000 ) ) ;
#101764=DIRECTION ( 'NONE',  ( 0.6830127018922180770, -0.6830127018922204085, -0.2588190451025213501 ) ) ;
#101765=VERTEX_POINT ( 'NONE', #46560 ) ;
#101766=ORIENTED_EDGE ( 'NONE', *, *, #94714, .T. ) ;
#101767=LINE ( 'NONE', #47450, #42656 ) ;
#101769=ADVANCED_FACE ( 'NONE', ( #102339 ), #66838, .T. ) ;
#101770=ADVANCED_FACE ( 'NONE', ( #24046 ), #121897, .F. ) ;
#101771=CARTESIAN_POINT ( 'NONE',  ( -5.700255128608413102, -27.71228299555201957, 4.000000000000000000 ) ) ;
#101772=ORIENTED_EDGE ( 'NONE', *, *, #88721, .F. ) ;
#101773=DIRECTION ( 'NONE',  ( -0.6830127018922181881, 0.6830127018922202975, -0.2588190451025214056 ) ) ;
#101775=CARTESIAN_POINT ( 'NONE',  ( 62.99451991528749772, 28.92564299267982264, 4.000000000000000000 ) ) ;
#101776=CARTESIAN_POINT ( 'NONE',  ( -32.29289321881323360, 20.25929247661551003, 5.000000000000000000 ) ) ;
#101778=AXIS2_PLACEMENT_3D ( 'NONE', #54908, #75243, #97675 ) ;
#101779=AXIS2_PLACEMENT_3D ( 'NONE', #123385, #58143, #124778 ) ;
#101781=EDGE_CURVE ( 'NONE', #51968, #46484, #13134, .T. ) ;
#101782=DIRECTION ( 'NONE',  ( 0.7071067811865486830, -0.7071067811865464625, -0.000000000000000000 ) ) ;
#101783=AXIS2_PLACEMENT_3D ( 'NONE', #128667, #49710, #107615 ) ;
#101784=FACE_OUTER_BOUND ( 'NONE', #27821, .T. ) ;
#101785=EDGE_CURVE ( 'NONE', #75355, #18399, #79899, .T. ) ;
#101786=CARTESIAN_POINT ( 'NONE',  ( 23.20710678118638981, -11.24070752338417201, 5.000000000000000000 ) ) ;
#101787=ORIENTED_EDGE ( 'NONE', *, *, #52070, .T. ) ;
#101788=ADVANCED_FACE ( 'NONE', ( #124074 ), #101585, .F. ) ;
#101789=ORIENTED_EDGE ( 'NONE', *, *, #20617, .T. ) ;
#101791=CARTESIAN_POINT ( 'NONE',  ( 0.000000000000000000, 0.000000000000000000, 5.000000000000000000 ) ) ;
#101793=CARTESIAN_POINT ( 'NONE',  ( 30.48921356237309510, -27.52281430457076894, 5.000000000000000000 ) ) ;
#101794=EDGE_CURVE ( 'NONE', #98472, #42161, #45123, .T. ) ;
#101795=VECTOR ( 'NONE', #63318, 1000.000000000000000 ) ;
#101796=CARTESIAN_POINT ( 'NONE',  ( 7.499999999999947597, -19.53360074219753884, 5.000000000000000000 ) ) ;
#101797=CARTESIAN_POINT ( 'NONE',  ( 75.29974487139158157, -27.71228299555258445, 4.000000000000000000 ) ) ;
#101798=ADVANCED_FACE ( 'NONE', ( #88605 ), #11698, .F. ) ;
#101799=LINE ( 'NONE', #132323, #127865 ) ;
#101800=VERTEX_POINT ( 'NONE', #89300 ) ;
#101802=CARTESIAN_POINT ( 'NONE',  ( 12.18398860626900060, 28.73617430169795739, 5.000000000000000000 ) ) ;
#101803=AXIS2_PLACEMENT_3D ( 'NONE', #111650, #132723, #113051 ) ;
#101804=AXIS2_PLACEMENT_3D ( 'NONE', #120907, #63706, #140515 ) ;
#101805=EDGE_CURVE ( 'NONE', #128291, #66418, #68993, .T. ) ;
#101808=DIRECTION ( 'NONE',  ( 0.7071067811865487940, 0.7071067811865463515, -0.000000000000000000 ) ) ;
#101809=VECTOR ( 'NONE', #109876, 1000.000000000000000 ) ;
#101810=DIRECTION ( 'NONE',  ( 0.6830127018922180770, 0.6830127018922202975, -0.2588190451025213501 ) ) ;
#101813=CARTESIAN_POINT ( 'NONE',  ( -5.241399257802002332, 21.72500000000000853, 5.000000000000000000 ) ) ;
#101814=ORIENTED_EDGE ( 'NONE', *, *, #57461, .F. ) ;
#101815=ADVANCED_FACE ( 'NONE', ( #35674 ), #118550, .F. ) ;
#101817=VECTOR ( 'NONE', #43216, 1000.000000000000000 ) ;
#101819=VECTOR ( 'NONE', #46230, 999.9999999999998863 ) ;
#101820=DIRECTION ( 'NONE',  ( 0.7071067811865486830, -0.7071067811865464625, -0.000000000000000000 ) ) ;
#101822=LINE ( 'NONE', #125000, #9169 ) ;
#101823=CARTESIAN_POINT ( 'NONE',  ( 3.096670641874039287, -2.240707523384260824, 15.26439735382753149 ) ) ;
#101824=CARTESIAN_POINT ( 'NONE',  ( 26.28769006033953914, -21.73547319004781286, 4.999917730833664642 ) ) ;
#101826=VERTEX_POINT ( 'NONE', #19250 ) ;
#101827=ORIENTED_EDGE ( 'NONE', *, *, #8861, .T. ) ;
#101828=DIRECTION ( 'NONE',  ( 0.7071067811865487940, -0.7071067811865463515, 0.000000000000000000 ) ) ;
#101829=CARTESIAN_POINT ( 'NONE',  ( 0.1839886062690032631, 28.73617430169787568, 5.000000000000000000 ) ) ;
#101832=CARTESIAN_POINT ( 'NONE',  ( 78.18398860626899705, 28.73617430169841924, 5.000000000000000000 ) ) ;
#101835=EDGE_CURVE ( 'NONE', #94364, #3251, #119950, .T. ) ;
#101836=CARTESIAN_POINT ( 'NONE',  ( -19.49999999999986500, -12.08601207473291161, -10.46905243149090481 ) ) ;
#101837=EDGE_LOOP ( 'NONE', ( #3226, #64304, #142507, #564 ) ) ;
#101839=LINE ( 'NONE', #115523, #79325 ) ;
#101840=CARTESIAN_POINT ( 'NONE',  ( 72.48921356237309510, -27.52281430457106026, 5.000000000000000000 ) ) ;
#101842=AXIS2_PLACEMENT_3D ( 'NONE', #60856, #75806, #104282 ) ;
#101843=ORIENTED_EDGE ( 'NONE', *, *, #79343, .F. ) ;
#101844=EDGE_CURVE ( 'NONE', #52145, #11858, #63506, .T. ) ;
#101845=DIRECTION ( 'NONE',  ( -0.7071067811865487940, 0.7071067811865463515, 0.000000000000000000 ) ) ;
#101849=EDGE_LOOP ( 'NONE', ( #14549, #130314, #96920, #51322 ) ) ;
#101850=VERTEX_POINT ( 'NONE', #75787 ) ;
#101851=VECTOR ( 'NONE', #140788, 1000.000000000000227 ) ;
#101852=CARTESIAN_POINT ( 'NONE',  ( -33.51665438641022376, 22.22500000000000142, 4.500000000000000888 ) ) ;
#101853=LINE ( 'NONE', #22828, #141533 ) ;
#101854=LINE ( 'NONE', #1778, #74184 ) ;
#101855=DIRECTION ( 'NONE',  ( 0.6830127018922181881, 0.6830127018922202975, -0.2588190451025214056 ) ) ;
#101857=ORIENTED_EDGE ( 'NONE', *, *, #132612, .T. ) ;
#101858=DIRECTION ( 'NONE',  ( 0.7071067811865487940, -0.7071067811865463515, 0.000000000000000000 ) ) ;
#101859=DIRECTION ( 'NONE',  ( 1.000000000000000000, 0.000000000000000000, 0.000000000000000000 ) ) ;
#101860=DIRECTION ( 'NONE',  ( -0.7071067811865486830, -0.7071067811865464625, -0.000000000000000000 ) ) ;
#101862=EDGE_LOOP ( 'NONE', ( #55830, #38113, #48576, #59575 ) ) ;
#101863=ORIENTED_EDGE ( 'NONE', *, *, #94382, .F. ) ;
#101869=CARTESIAN_POINT ( 'NONE',  ( -39.48921356237310221, -27.52281430457082934, 5.000000000000000000 ) ) ;
#101870=CARTESIAN_POINT ( 'NONE',  ( -34.49999999999975842, 4.464255608400450548, 4.994342998332166772 ) ) ;
#101871=ORIENTED_EDGE ( 'NONE', *, *, #127631, .F. ) ;
#101872=ORIENTED_EDGE ( 'NONE', *, *, #82652, .T. ) ;
#101875=VECTOR ( 'NONE', #92659, 999.9999999999998863 ) ;
#101879=CARTESIAN_POINT ( 'NONE',  ( 14.60438740478481989, -0.8081507193758268315, 4.000000000000000000 ) ) ;
#101880=VECTOR ( 'NONE', #68979, 1000.000000000000000 ) ;
#101881=AXIS2_PLACEMENT_3D ( 'NONE', #104459, #70471, #25465 ) ;
#101883=ORIENTED_EDGE ( 'NONE', *, *, #134458, .T. ) ;
#101885=ADVANCED_FACE ( 'NONE', ( #76510 ), #20658, .T. ) ;
#101886=EDGE_CURVE ( 'NONE', #47321, #30178, #53293, .T. ) ;
#101887=FACE_BOUND ( 'NONE', #143317, .T. ) ;
#101888=LINE ( 'NONE', #67132, #105777 ) ;
#101889=DIRECTION ( 'NONE',  ( 0.7071067811865486830, -0.7071067811865464625, -0.000000000000000000 ) ) ;
#101890=FACE_OUTER_BOUND ( 'NONE', #59579, .T. ) ;
#101891=VECTOR ( 'NONE', #49075, 999.9999999999998863 ) ;
#101893=EDGE_CURVE ( 'NONE', #103695, #97839, #52582, .T. ) ;
#101894=ADVANCED_FACE ( 'NONE', ( #64913 ), #85204, .F. ) ;
#101895=CARTESIAN_POINT ( 'NONE',  ( 0.000000000000000000, 0.000000000000000000, 5.000000000000000000 ) ) ;
#101897=ORIENTED_EDGE ( 'NONE', *, *, #124018, .T. ) ;
#101900=ORIENTED_EDGE ( 'NONE', *, *, #47864, .T. ) ;
#101902=CARTESIAN_POINT ( 'NONE',  ( -15.18398860626900237, 28.73617430169797871, 5.000000000000000000 ) ) ;
#101903=VERTEX_POINT ( 'NONE', #9789 ) ;
#101904=VECTOR ( 'NONE', #105727, 1000.000000000000000 ) ;
#101905=FACE_OUTER_BOUND ( 'NONE', #84104, .T. ) ;
#101906=DIRECTION ( 'NONE',  ( -0.7071067811865486830, -0.7071067811865464625, 0.000000000000000000 ) ) ;
#101907=ADVANCED_FACE ( 'NONE', ( #109098 ), #96760, .T. ) ;
#101908=VECTOR ( 'NONE', #42335, 1000.000000000000000 ) ;
#101909=DIRECTION ( 'NONE',  ( 0.7071067811865487940, 0.7071067811865463515, 0.000000000000000000 ) ) ;
#101910=EDGE_LOOP ( 'NONE', ( #55821, #120733, #24929, #120863 ) ) ;
#101911=CARTESIAN_POINT ( 'NONE',  ( 21.79289321881330821, -14.24070752338414003, 5.000000000000000000 ) ) ;
#101912=DIRECTION ( 'NONE',  ( 0.3543493200069162685, -0.000000000000000000, -0.9351131265310288487 ) ) ;
#101913=LINE ( 'NONE', #2575, #140664 ) ;
#101914=CARTESIAN_POINT ( 'NONE',  ( -26.99999999999980815, -3.412538124160723108, 4.000000000000000000 ) ) ;
#101915=VECTOR ( 'NONE', #33747, 1000.000000000000000 ) ;
#101916=CARTESIAN_POINT ( 'NONE',  ( 10.49999999999992362, 21.05218569542895679, 5.000000000000000000 ) ) ;
#101917=ADVANCED_FACE ( 'NONE', ( #30113 ), #40320, .T. ) ;
#101918=PLANE ( 'NONE',  #69979 ) ;
#101919=EDGE_LOOP ( 'NONE', ( #103154, #90680, #87137, #41939 ) ) ;
#101920=AXIS2_PLACEMENT_3D ( 'NONE', #72471, #60142, #104308 ) ;
#101921=DIRECTION ( 'NONE',  ( -0.7071067811865487940, 0.7071067811865463515, -0.000000000000000000 ) ) ;
#101922=DIRECTION ( 'NONE',  ( 0.3543493200069163240, -0.000000000000000000, 0.9351131265310288487 ) ) ;
#101923=ORIENTED_EDGE ( 'NONE', *, *, #7999, .F. ) ;
#101924=ORIENTED_EDGE ( 'NONE', *, *, #86387, .F. ) ;
#101925=VECTOR ( 'NONE', #44786, 1000.000000000000000 ) ;
#101928=EDGE_CURVE ( 'NONE', #44583, #143262, #54060, .T. ) ;
#101929=ORIENTED_EDGE ( 'NONE', *, *, #41601, .T. ) ;
#101933=CARTESIAN_POINT ( 'NONE',  ( -24.48921356237309510, -27.52281430457072631, 5.000000000000000000 ) ) ;
#101934=ORIENTED_EDGE ( 'NONE', *, *, #114068, .F. ) ;
#101935=FACE_OUTER_BOUND ( 'NONE', #4486, .T. ) ;
#101936=EDGE_CURVE ( 'NONE', #49860, #142463, #41718, .T. ) ;
#101937=ORIENTED_EDGE ( 'NONE', *, *, #70482, .T. ) ;
#101938=LINE ( 'NONE', #37399, #101991 ) ;
#101939=AXIS2_PLACEMENT_3D ( 'NONE', #114123, #59079, #125736 ) ;
#101941=ORIENTED_EDGE ( 'NONE', *, *, #45534, .T. ) ;
#101942=CARTESIAN_POINT ( 'NONE',  ( 29.99451991528749417, 28.92564299267958816, 4.000000000000000000 ) ) ;
#101943=LINE ( 'NONE', #35294, #140935 ) ;
#101946=EDGE_CURVE ( 'NONE', #110269, #27958, #141763, .T. ) ;
#101947=ORIENTED_EDGE ( 'NONE', *, *, #124068, .F. ) ;
#101948=CARTESIAN_POINT ( 'NONE',  ( 19.00193056682084247, -22.22500000000000142, 4.500000000000000888 ) ) ;
#101949=ORIENTED_EDGE ( 'NONE', *, *, #40129, .T. ) ;
#101950=ORIENTED_EDGE ( 'NONE', *, *, #57503, .T. ) ;
#101951=ORIENTED_EDGE ( 'NONE', *, *, #61266, .F. ) ;
#101952=LINE ( 'NONE', #3327, #37809 ) ;
#101954=EDGE_CURVE ( 'NONE', #122361, #96060, #130892, .T. ) ;
#101955=CARTESIAN_POINT ( 'NONE',  ( 13.21321903303351242, 12.75929247661559351, 10.29404684609038334 ) ) ;
#101956=EDGE_CURVE ( 'NONE', #61607, #37747, #18500, .T. ) ;
#101957=DIRECTION ( 'NONE',  ( 0.7071067811865487940, 0.7071067811865463515, 0.000000000000000000 ) ) ;
#101958=DIRECTION ( 'NONE',  ( -0.3543493200069162685, -0.000000000000000000, -0.9351131265310288487 ) ) ;
#101960=VECTOR ( 'NONE', #101273, 1000.000000000000227 ) ;
#101961=VECTOR ( 'NONE', #39209, 1000.000000000000000 ) ;
#101962=CARTESIAN_POINT ( 'NONE',  ( 24.48921356237309510, -27.52281430457072631, 5.000000000000000000 ) ) ;
#101964=CARTESIAN_POINT ( 'NONE',  ( 30.29177708983029405, -15.74070752338411339, 19.73771281079104156 ) ) ;
#101965=CARTESIAN_POINT ( 'NONE',  ( -23.42830866441053317, 7.233000843196644603, 4.333645886165178318 ) ) ;
#101966=EDGE_CURVE ( 'NONE', #133473, #83408, #96078, .T. ) ;
#101967=LINE ( 'NONE', #2634, #21145 ) ;
#101968=ORIENTED_EDGE ( 'NONE', *, *, #25258, .F. ) ;
#101969=ORIENTED_EDGE ( 'NONE', *, *, #191, .T. ) ;
#101970=EDGE_LOOP ( 'NONE', ( #24335, #131915, #119520, #12677 ) ) ;
#101971=DIRECTION ( 'NONE',  ( -0.6830127018922180770, -0.6830127018922204085, -0.2588190451025213501 ) ) ;
#101972=CARTESIAN_POINT ( 'NONE',  ( 13.49999999999990052, -12.08601207473287964, -10.46905243149097409 ) ) ;
#101973=VECTOR ( 'NONE', #110979, 999.9999999999998863 ) ;
#101978=VECTOR ( 'NONE', #119849, 1000.000000000000000 ) ;
#101979=DIRECTION ( 'NONE',  ( 0.6830127018922180770, -0.6830127018922204085, -0.2588190451025213501 ) ) ;
#101980=CARTESIAN_POINT ( 'NONE',  ( -19.05000000000000071, 3.174999999999997158, 4.000000000000000000 ) ) ;
#101981=LINE ( 'NONE', #24418, #97618 ) ;
#101982=PLANE ( 'NONE',  #88295 ) ;
#101984=ORIENTED_EDGE ( 'NONE', *, *, #22878, .F. ) ;
#101985=AXIS2_PLACEMENT_3D ( 'NONE', #24559, #103527, #9766 ) ;
#101986=VECTOR ( 'NONE', #1911, 1000.000000000000000 ) ;
#101987=VECTOR ( 'NONE', #142628, 1000.000000000000000 ) ;
#101990=VERTEX_POINT ( 'NONE', #43869 ) ;
#101991=VECTOR ( 'NONE', #114238, 999.9999999999998863 ) ;
#101992=CARTESIAN_POINT ( 'NONE',  ( 16.17183060077635659, -2.240707523384260824, 4.000000000000000000 ) ) ;
#101993=CARTESIAN_POINT ( 'NONE',  ( -34.47516574401892342, 15.02806734111566733, 4.998110765256835286 ) ) ;
#101994=ORIENTED_EDGE ( 'NONE', *, *, #2270, .F. ) ;
#101995=CARTESIAN_POINT ( 'NONE',  ( 34.92499999999998295, 21.00612307739175222, 4.000000000000000000 ) ) ;
#101996=PLANE ( 'NONE',  #54163 ) ;
#101997=EDGE_LOOP ( 'NONE', ( #69433, #53851, #95424, #134260 ) ) ;
#101998=CARTESIAN_POINT ( 'NONE',  ( -12.48921356237309155, -27.52281430457064104, 5.000000000000000000 ) ) ;
#101999=ORIENTED_EDGE ( 'NONE', *, *, #88071, .T. ) ;
#102002=ORIENTED_EDGE ( 'NONE', *, *, #58480, .F. ) ;
#102003=CARTESIAN_POINT ( 'NONE',  ( 6.712309939660229041, -21.73547319004781286, 4.999917730833665530 ) ) ;
#102006=CARTESIAN_POINT ( 'NONE',  ( 19.30725242247703122, 9.139235811853160030, 4.261625515810899323 ) ) ;
#102007=ORIENTED_EDGE ( 'NONE', *, *, #52460, .T. ) ;
#102008=DIRECTION ( 'NONE',  ( -0.7071067811865487940, 0.7071067811865463515, -0.000000000000000000 ) ) ;
#102009=CARTESIAN_POINT ( 'NONE',  ( 18.48921356237309510, -27.52281430457068367, 5.000000000000000000 ) ) ;
#102010=LINE ( 'NONE', #36061, #60041 ) ;
#102013=AXIS2_PLACEMENT_3D ( 'NONE', #46213, #90389, #134638 ) ;
#102014=FACE_OUTER_BOUND ( 'NONE', #41996, .T. ) ;
#102017=AXIS2_PLACEMENT_3D ( 'NONE', #93679, #5906, #50179 ) ;
#102018=DIRECTION ( 'NONE',  ( 0.7071067811865487940, -0.7071067811865463515, 0.000000000000000000 ) ) ;
#102019=ORIENTED_EDGE ( 'NONE', *, *, #96343, .T. ) ;
#102022=VECTOR ( 'NONE', #21945, 1000.000000000000000 ) ;
#102023=LINE ( 'NONE', #65867, #131141 ) ;
#102024=FACE_OUTER_BOUND ( 'NONE', #128878, .T. ) ;
#102026=DIRECTION ( 'NONE',  ( -0.6830127018922180770, -0.6830127018922204085, -0.2588190451025213501 ) ) ;
#102027=VERTEX_POINT ( 'NONE', #67799 ) ;
#102028=AXIS2_PLACEMENT_3D ( 'NONE', #82388, #17797, #80955 ) ;
#102029=DIRECTION ( 'NONE',  ( 0.7071067811865487940, 0.7071067811865463515, 0.000000000000000000 ) ) ;
#102030=FACE_OUTER_BOUND ( 'NONE', #130316, .T. ) ;
#102031=CARTESIAN_POINT ( 'NONE',  ( 36.29974487139159578, -27.71228299555231445, 4.000000000000000000 ) ) ;
#102032=ORIENTED_EDGE ( 'NONE', *, *, #110021, .T. ) ;
#102033=CARTESIAN_POINT ( 'NONE',  ( 24.75149461641275295, 4.949500604449032615, 4.299609778361314305 ) ) ;
#102035=CARTESIAN_POINT ( 'NONE',  ( 12.70710678118645909, 5.259292476615661016, 5.000000000000000000 ) ) ;
#102036=ORIENTED_EDGE ( 'NONE', *, *, #53964, .F. ) ;
#102037=PLANE ( 'NONE',  #43991 ) ;
#102038=DIRECTION ( 'NONE',  ( 1.000000000000000000, 0.000000000000000000, 0.000000000000000000 ) ) ;
#102039=CARTESIAN_POINT ( 'NONE',  ( 36.48921356237310221, -27.52281430457080802, 5.000000000000000000 ) ) ;
#102040=CARTESIAN_POINT ( 'NONE',  ( 6.183988606268994381, 28.73617430169791476, 5.000000000000000000 ) ) ;
#102042=ORIENTED_EDGE ( 'NONE', *, *, #7903, .F. ) ;
#102043=ORIENTED_EDGE ( 'NONE', *, *, #116715, .F. ) ;
#102044=EDGE_LOOP ( 'NONE', ( #108496, #69773, #40034, #79607 ) ) ;
#102046=VECTOR ( 'NONE', #18327, 1000.000000000000000 ) ;
#102050=FACE_OUTER_BOUND ( 'NONE', #63242, .T. ) ;
#102053=DIRECTION ( 'NONE',  ( -0.7071067811865487940, 0.7071067811865463515, -0.000000000000000000 ) ) ;
#102054=DIRECTION ( 'NONE',  ( -0.6830127018922181881, 0.6830127018922202975, -0.2588190451025214056 ) ) ;
#102055=LINE ( 'NONE', #100640, #127438 ) ;
#102057=VERTEX_POINT ( 'NONE', #111989 ) ;
#102058=CARTESIAN_POINT ( 'NONE',  ( -13.17183060077637435, 21.75929247661549581, 4.000000000000000000 ) ) ;
#102060=LINE ( 'NONE', #1292, #26106 ) ;
#102061=ORIENTED_EDGE ( 'NONE', *, *, #77573, .T. ) ;
#102062=ORIENTED_EDGE ( 'NONE', *, *, #54497, .T. ) ;
#102063=EDGE_CURVE ( 'NONE', #116772, #119169, #318, .T. ) ;
#102064=PLANE ( 'NONE',  #132639 ) ;
#102065=EDGE_CURVE ( 'NONE', #30212, #49717, #109827, .T. ) ;
#102066=EDGE_CURVE ( 'NONE', #83184, #11113, #56211, .T. ) ;
#102067=DIRECTION ( 'NONE',  ( -0.7071067811865487940, 0.7071067811865463515, -0.000000000000000000 ) ) ;
#102069=CARTESIAN_POINT ( 'NONE',  ( -27.18398860626900060, 28.73617430169806042, 5.000000000000000000 ) ) ;
#102070=VECTOR ( 'NONE', #23364, 999.9999999999998863 ) ;
#102072=CARTESIAN_POINT ( 'NONE',  ( -13.39656807105348690, -14.24070752338412937, 19.24067776001722763 ) ) ;
#102073=CARTESIAN_POINT ( 'NONE',  ( -39.48921356237310221, -27.52281430457082934, 5.000000000000000000 ) ) ;
#102074=EDGE_CURVE ( 'NONE', #127030, #100787, #22087, .T. ) ;
#102076=CARTESIAN_POINT ( 'NONE',  ( 22.49999999999984013, -13.53360074219759746, 5.000000000000000000 ) ) ;
#102078=ORIENTED_EDGE ( 'NONE', *, *, #95436, .T. ) ;
#102079=ORIENTED_EDGE ( 'NONE', *, *, #90482, .F. ) ;
#102080=LINE ( 'NONE', #113653, #131302 ) ;
#102082=EDGE_LOOP ( 'NONE', ( #21127, #54566, #42203, #121331 ) ) ;
#102083=ORIENTED_EDGE ( 'NONE', *, *, #80202, .T. ) ;
#102084=EDGE_CURVE ( 'NONE', #19532, #56087, #13346, .T. ) ;
#102085=AXIS2_PLACEMENT_3D ( 'NONE', #41319, #44214, #132669 ) ;
#102087=AXIS2_PLACEMENT_3D ( 'NONE', #48986, #94596, #114220 ) ;
#102088=EDGE_CURVE ( 'NONE', #134621, #58130, #35150, .T. ) ;
#102089=VECTOR ( 'NONE', #6263, 1000.000000000000000 ) ;
#102090=CARTESIAN_POINT ( 'NONE',  ( 11.51078643762690490, -27.52281430457047406, 5.000000000000000000 ) ) ;
#102091=ORIENTED_EDGE ( 'NONE', *, *, #99812, .T. ) ;
#102092=DIRECTION ( 'NONE',  ( -0.6830127018922180770, -0.6830127018922204085, -0.2588190451025213501 ) ) ;
#102093=CARTESIAN_POINT ( 'NONE',  ( -0.005480084712502889671, 28.92564299267938210, 4.000000000000000000 ) ) ;
#102094=CARTESIAN_POINT ( 'NONE',  ( -34.92500000000001137, 17.71849043720405348, 4.759050581649335143 ) ) ;
#102095=VECTOR ( 'NONE', #42257, 1000.000000000000227 ) ;
#102096=VECTOR ( 'NONE', #75107, 1000.000000000000227 ) ;
#102097=VECTOR ( 'NONE', #60658, 999.9999999999998863 ) ;
#102098=VECTOR ( 'NONE', #52989, 1000.000000000000227 ) ;
#102100=LINE ( 'NONE', #80364, #53706 ) ;
#102101=ORIENTED_EDGE ( 'NONE', *, *, #87568, .F. ) ;
#102102=VECTOR ( 'NONE', #70766, 1000.000000000000227 ) ;
#102106=ORIENTED_EDGE ( 'NONE', *, *, #13788, .T. ) ;
#102108=ORIENTED_EDGE ( 'NONE', *, *, #114682, .F. ) ;
#102109=EDGE_LOOP ( 'NONE', ( #28227, #124859, #81710, #140555 ) ) ;
#102110=DIRECTION ( 'NONE',  ( -0.7071067811865486830, -0.7071067811865464625, 0.000000000000000000 ) ) ;
#102112=EDGE_LOOP ( 'NONE', ( #120566, #83852, #134920, #18779, #4560 ) ) ;
#102113=VECTOR ( 'NONE', #63008, 1000.000000000000000 ) ;
#102114=EDGE_CURVE ( 'NONE', #66021, #103933, #122115, .T. ) ;
#102115=ORIENTED_EDGE ( 'NONE', *, *, #64125, .T. ) ;
#102117=LINE ( 'NONE', #126012, #135473 ) ;
#102118=LINE ( 'NONE', #100688, #11252 ) ;
#102121=LINE ( 'NONE', #91261, #42590 ) ;
#102122=AXIS2_PLACEMENT_3D ( 'NONE', #25040, #114200, #3286 ) ;
#102123=CARTESIAN_POINT ( 'NONE',  ( -33.48921356237309510, -27.52281430457078670, 5.000000000000000000 ) ) ;
#102124=EDGE_CURVE ( 'NONE', #84513, #81345, #89500, .T. ) ;
#102125=AXIS2_PLACEMENT_3D ( 'NONE', #15480, #18151, #140670 ) ;
#102126=DIRECTION ( 'NONE',  ( 0.7071067811865487940, -0.7071067811865463515, 0.000000000000000000 ) ) ;
#102127=VECTOR ( 'NONE', #131501, 1000.000000000000000 ) ;
#102129=EDGE_CURVE ( 'NONE', #135680, #39409, #24253, .T. ) ;
#102130=ORIENTED_EDGE ( 'NONE', *, *, #31773, .F. ) ;
#102131=VECTOR ( 'NONE', #117690, 999.9999999999998863 ) ;
#102133=LINE ( 'NONE', #78239, #114726 ) ;
#102134=ORIENTED_EDGE ( 'NONE', *, *, #34327, .F. ) ;
#102136=VECTOR ( 'NONE', #55764, 1000.000000000000000 ) ;
#102137=EDGE_LOOP ( 'NONE', ( #62991, #33462, #43718, #109251, #96713 ) ) ;
#102138=DIRECTION ( 'NONE',  ( 0.7071067811865487940, 0.7071067811865463515, -0.000000000000000000 ) ) ;
#102140=VECTOR ( 'NONE', #106594, 1000.000000000000000 ) ;
#102141=ADVANCED_FACE ( 'NONE', ( #33723 ), #68499, .F. ) ;
#102142=FACE_OUTER_BOUND ( 'NONE', #110827, .T. ) ;
#102143=CARTESIAN_POINT ( 'NONE',  ( -54.18398860626899705, 28.73617430169825226, 5.000000000000000000 ) ) ;
#102145=LINE ( 'NONE', #34742, #26423 ) ;
#102146=CARTESIAN_POINT ( 'NONE',  ( 0.1839886062690032631, 28.73617430169787568, 5.000000000000000000 ) ) ;
#102147=EDGE_LOOP ( 'NONE', ( #137976, #41890, #10920, #78050 ) ) ;
#102148=LINE ( 'NONE', #2804, #53529 ) ;
#102149=ORIENTED_EDGE ( 'NONE', *, *, #38317, .T. ) ;
#102150=EDGE_CURVE ( 'NONE', #29906, #114615, #66346, .T. ) ;
#102151=LINE ( 'NONE', #134061, #127866 ) ;
#102152=VECTOR ( 'NONE', #95464, 1000.000000000000000 ) ;
#102155=CARTESIAN_POINT ( 'NONE',  ( -13.49999999999989697, -14.94781430457067550, 5.000000000000000000 ) ) ;
#102156=EDGE_CURVE ( 'NONE', #112560, #117136, #77237, .T. ) ;
#102158=VERTEX_POINT ( 'NONE', #48151 ) ;
#102159=ORIENTED_EDGE ( 'NONE', *, *, #32080, .T. ) ;
#102161=ORIENTED_EDGE ( 'NONE', *, *, #88746, .T. ) ;
#102163=FACE_OUTER_BOUND ( 'NONE', #54545, .T. ) ;
#102164=CARTESIAN_POINT ( 'NONE',  ( -23.70822291016937911, -15.74070752338412404, 19.73771281079092077 ) ) ;
#102166=CARTESIAN_POINT ( 'NONE',  ( -21.00548008471250938, 28.92564299267923644, 4.000000000000000000 ) ) ;
#102167=ORIENTED_EDGE ( 'NONE', *, *, #2197, .F. ) ;
#102168=FACE_OUTER_BOUND ( 'NONE', #57682, .T. ) ;
#102169=LINE ( 'NONE', #79004, #15584 ) ;
#102170=CARTESIAN_POINT ( 'NONE',  ( -8.816011393731004731, 28.73617430169781173, 5.000000000000000000 ) ) ;
#102171=DIRECTION ( 'NONE',  ( -0.000000000000000000, -0.3543493200069152693, 0.9351131265310292928 ) ) ;
#102174=AXIS2_PLACEMENT_3D ( 'NONE', #50103, #26204, #37063 ) ;
#102175=CARTESIAN_POINT ( 'NONE',  ( 29.67183060077626067, 8.259292476615637923, 4.000000000000000000 ) ) ;
#102177=ORIENTED_EDGE ( 'NONE', *, *, #84109, .T. ) ;
#102178=ADVANCED_FACE ( 'NONE', ( #38697 ), #114791, .F. ) ;
#102180=ADVANCED_FACE ( 'NONE', ( #71334 ), #82229, .F. ) ;
#102181=CARTESIAN_POINT ( 'NONE',  ( -30.18398860626900060, 28.73617430169808173, 5.000000000000000000 ) ) ;
#102182=LINE ( 'NONE', #68164, #39104 ) ;
#102183=VECTOR ( 'NONE', #32682, 1000.000000000000227 ) ;
#102184=ORIENTED_EDGE ( 'NONE', *, *, #69206, .T. ) ;
#102186=ORIENTED_EDGE ( 'NONE', *, *, #14808, .T. ) ;
#102187=DIRECTION ( 'NONE',  ( -0.000000000000000000, 0.3543493200069152138, -0.9351131265310292928 ) ) ;
#102189=PLANE ( 'NONE',  #124880 ) ;
#102190=LINE ( 'NONE', #136220, #34675 ) ;
#102191=FACE_OUTER_BOUND ( 'NONE', #14604, .T. ) ;
#102192=CARTESIAN_POINT ( 'NONE',  ( -13.49999999999991473, -12.08601207473291161, -10.46905243149091547 ) ) ;
#102193=CARTESIAN_POINT ( 'NONE',  ( 63.18398860626900415, 28.73617430169831621, 5.000000000000000000 ) ) ;
#102194=DIRECTION ( 'NONE',  ( -0.7071067811865486830, -0.7071067811865464625, 0.000000000000000000 ) ) ;
#102196=CARTESIAN_POINT ( 'NONE',  ( -14.29289321881335795, -3.740707523384239952, 5.000000000000000000 ) ) ;
#102197=DIRECTION ( 'NONE',  ( 1.000000000000000000, 0.000000000000000000, 0.000000000000000000 ) ) ;
#102199=LINE ( 'NONE', #36915, #65205 ) ;
#102200=CARTESIAN_POINT ( 'NONE',  ( 0.000000000000000000, 0.000000000000000000, 5.000000000000000000 ) ) ;
#102201=ORIENTED_EDGE ( 'NONE', *, *, #14061, .T. ) ;
#102202=EDGE_CURVE ( 'NONE', #134912, #21649, #138013, .T. ) ;
#102203=ORIENTED_EDGE ( 'NONE', *, *, #98631, .T. ) ;
#102204=VECTOR ( 'NONE', #137246, 1000.000000000000000 ) ;
#102207=EDGE_CURVE ( 'NONE', #76282, #53303, #80783, .T. ) ;
#102208=EDGE_LOOP ( 'NONE', ( #47110, #136382, #141590, #62502 ) ) ;
#102209=ORIENTED_EDGE ( 'NONE', *, *, #110445, .F. ) ;
#102210=ORIENTED_EDGE ( 'NONE', *, *, #17744, .T. ) ;
#102211=DIRECTION ( 'NONE',  ( -0.7071067811865487940, 0.7071067811865463515, 0.000000000000000000 ) ) ;
#102213=AXIS2_PLACEMENT_3D ( 'NONE', #20287, #94988, #64526 ) ;
#102216=VECTOR ( 'NONE', #59301, 1000.000000000000227 ) ;
#102218=VERTEX_POINT ( 'NONE', #91645 ) ;
#102219=LINE ( 'NONE', #94861, #78753 ) ;
#102220=VECTOR ( 'NONE', #40116, 1000.000000000000000 ) ;
#102221=LINE ( 'NONE', #58020, #106561 ) ;
#102222=DIRECTION ( 'NONE',  ( -0.3543493200069162685, -0.000000000000000000, -0.9351131265310288487 ) ) ;
#102224=EDGE_CURVE ( 'NONE', #134353, #40105, #36548, .T. ) ;
#102226=LINE ( 'NONE', #123271, #130410 ) ;
#102227=LINE ( 'NONE', #135564, #54319 ) ;
#102229=LINE ( 'NONE', #2880, #95353 ) ;
#102233=FACE_OUTER_BOUND ( 'NONE', #101728, .T. ) ;
#102234=PLANE ( 'NONE',  #39964 ) ;
#102235=ORIENTED_EDGE ( 'NONE', *, *, #96319, .T. ) ;
#102236=ORIENTED_EDGE ( 'NONE', *, *, #179, .F. ) ;
#102238=VERTEX_POINT ( 'NONE', #82925 ) ;
#102239=AXIS2_PLACEMENT_3D ( 'NONE', #79320, #92264, #68434 ) ;
#102240=CARTESIAN_POINT ( 'NONE',  ( -32.20710678118632586, 12.75929247661558463, 5.000000000000000000 ) ) ;
#102241=DIRECTION ( 'NONE',  ( 1.000000000000000000, 0.000000000000000000, 0.000000000000000000 ) ) ;
#102242=CARTESIAN_POINT ( 'NONE',  ( -15.00548008471250228, 28.92564299267927552, 4.000000000000000000 ) ) ;
#102243=VECTOR ( 'NONE', #92797, 999.9999999999998863 ) ;
#102244=VECTOR ( 'NONE', #86188, 999.9999999999998863 ) ;
#102247=VECTOR ( 'NONE', #138686, 1000.000000000000000 ) ;
#102248=EDGE_LOOP ( 'NONE', ( #78888, #57745, #99657, #68369 ) ) ;
#102249=CARTESIAN_POINT ( 'NONE',  ( -18.48921356237309510, -27.52281430457068367, 5.000000000000000000 ) ) ;
#102251=VECTOR ( 'NONE', #83291, 1000.000000000000227 ) ;
#102252=CARTESIAN_POINT ( 'NONE',  ( 12.18398860626900060, 28.73617430169795739, 5.000000000000000000 ) ) ;
#102253=ORIENTED_EDGE ( 'NONE', *, *, #40625, .T. ) ;
#102256=VECTOR ( 'NONE', #72825, 1000.000000000000000 ) ;
#102257=CARTESIAN_POINT ( 'NONE',  ( 63.18398860626900415, 28.73617430169831621, 5.000000000000000000 ) ) ;
#102258=ADVANCED_FACE ( 'NONE', ( #127111 ), #27810, .F. ) ;
#102259=EDGE_CURVE ( 'NONE', #11839, #99425, #126401, .T. ) ;
#102262=EDGE_CURVE ( 'NONE', #119015, #53073, #93786, .T. ) ;
#102263=ORIENTED_EDGE ( 'NONE', *, *, #2270, .T. ) ;
#102264=ORIENTED_EDGE ( 'NONE', *, *, #68622, .T. ) ;
#102266=EDGE_CURVE ( 'NONE', #129488, #61952, #14066, .T. ) ;
#102267=ORIENTED_EDGE ( 'NONE', *, *, #6788, .F. ) ;
#102268=VERTEX_POINT ( 'NONE', #69939 ) ;
#102269=VECTOR ( 'NONE', #123989, 1000.000000000000000 ) ;
#102270=VERTEX_POINT ( 'NONE', #4562 ) ;
#102271=AXIS2_PLACEMENT_3D ( 'NONE', #87898, #66170, #110339 ) ;
#102272=EDGE_CURVE ( 'NONE', #128989, #14082, #48869, .T. ) ;
#102273=LINE ( 'NONE', #102972, #63344 ) ;
#102274=EDGE_CURVE ( 'NONE', #60720, #104026, #125720, .T. ) ;
#102277=EDGE_LOOP ( 'NONE', ( #43194, #102293, #109508, #44983 ) ) ;
#102278=CARTESIAN_POINT ( 'NONE',  ( 25.82816939922335209, 15.75929247661555976, 4.000000000000000000 ) ) ;
#102279=AXIS2_PLACEMENT_3D ( 'NONE', #117233, #62916, #140439 ) ;
#102280=VECTOR ( 'NONE', #69915, 1000.000000000000000 ) ;
#102281=CARTESIAN_POINT ( 'NONE',  ( 17.67183060077634593, -3.740707523384244837, 4.000000000000000000 ) ) ;
#102282=PLANE ( 'NONE',  #37450 ) ;
#102283=EDGE_CURVE ( 'NONE', #92108, #91730, #5324, .T. ) ;
#102284=FACE_BOUND ( 'NONE', #140354, .T. ) ;
#102285=ORIENTED_EDGE ( 'NONE', *, *, #80475, .T. ) ;
#102286=ADVANCED_FACE ( 'NONE', ( #16942 ), #38001, .F. ) ;
#102288=DIRECTION ( 'NONE',  ( 0.7071067811865487940, 0.7071067811865463515, -0.000000000000000000 ) ) ;
#102290=ORIENTED_EDGE ( 'NONE', *, *, #48223, .F. ) ;
#102291=CARTESIAN_POINT ( 'NONE',  ( -34.47516574401891631, -16.50948238788421918, 4.998110765256836174 ) ) ;
#102292=VERTEX_POINT ( 'NONE', #59066 ) ;
#102293=ORIENTED_EDGE ( 'NONE', *, *, #93252, .T. ) ;
#102295=( BOUNDED_CURVE ( )  B_SPLINE_CURVE ( 3, ( #126454, #105416, #49662, #72139 ),
 .UNSPECIFIED., .F., .T. ) 
 B_SPLINE_CURVE_WITH_KNOTS ( ( 4, 4 ),
 ( 5.106027341939292086, 6.645403452391244414 ),
 .UNSPECIFIED. ) 
 CURVE ( )  GEOMETRIC_REPRESENTATION_ITEM ( )  RATIONAL_B_SPLINE_CURVE ( ( 1.000000000000000000, 0.8120851936182307274, 0.8120851936182307274, 1.000000000000000000 ) ) 
 REPRESENTATION_ITEM ( '' )  );
#102296=EDGE_CURVE ( 'NONE', #2768, #55124, #49604, .T. ) ;
#102297=ORIENTED_EDGE ( 'NONE', *, *, #59876, .T. ) ;
#102299=ORIENTED_EDGE ( 'NONE', *, *, #142873, .F. ) ;
#102300=DIRECTION ( 'NONE',  ( -0.6830127018922181881, 0.6830127018922202975, -0.2588190451025214056 ) ) ;
#102301=CARTESIAN_POINT ( 'NONE',  ( -5.999999999999956479, -0.8619312979532001151, -5.102805207349841332 ) ) ;
#102302=ORIENTED_EDGE ( 'NONE', *, *, #11518, .T. ) ;
#102303=DIRECTION ( 'NONE',  ( 1.000000000000000000, 0.000000000000000000, 0.000000000000000000 ) ) ;
#102304=AXIS2_PLACEMENT_3D ( 'NONE', #3868, #49600, #59750 ) ;
#102305=VECTOR ( 'NONE', #132099, 1000.000000000000000 ) ;
#102306=CARTESIAN_POINT ( 'NONE',  ( -9.299744871391588674, -27.71228299555212971, 4.000000000000000000 ) ) ;
#102307=VECTOR ( 'NONE', #140443, 1000.000000000000000 ) ;
#102308=VECTOR ( 'NONE', #52327, 999.9999999999998863 ) ;
#102310=DIRECTION ( 'NONE',  ( -0.7071067811865487940, 0.7071067811865463515, -0.000000000000000000 ) ) ;
#102312=VERTEX_POINT ( 'NONE', #37270 ) ;
#102313=EDGE_CURVE ( 'NONE', #130580, #83276, #129248, .T. ) ;
#102314=VERTEX_POINT ( 'NONE', #98072 ) ;
#102315=VECTOR ( 'NONE', #59787, 1000.000000000000227 ) ;
#102316=ORIENTED_EDGE ( 'NONE', *, *, #30820, .F. ) ;
#102317=VECTOR ( 'NONE', #519, 999.9999999999998863 ) ;
#102318=ORIENTED_EDGE ( 'NONE', *, *, #16872, .F. ) ;
#102319=AXIS2_PLACEMENT_3D ( 'NONE', #59819, #38767, #4637 ) ;
#102320=CARTESIAN_POINT ( 'NONE',  ( 25.82816939922335209, 3.759292476615676559, 4.000000000000000000 ) ) ;
#102321=VERTEX_POINT ( 'NONE', #141581 ) ;
#102322=ORIENTED_EDGE ( 'NONE', *, *, #110741, .F. ) ;
#102323=DIRECTION ( 'NONE',  ( -0.3543493200069163240, -0.000000000000000000, -0.9351131265310288487 ) ) ;
#102324=DIRECTION ( 'NONE',  ( -0.7071067811865487940, 0.7071067811865463515, -0.000000000000000000 ) ) ;
#102325=VERTEX_POINT ( 'NONE', #116958 ) ;
#102327=ORIENTED_EDGE ( 'NONE', *, *, #112583, .F. ) ;
#102328=ADVANCED_FACE ( 'NONE', ( #142307 ), #95920, .F. ) ;
#102329=DIRECTION ( 'NONE',  ( 0.6830127018922180770, -0.6830127018922204085, -0.2588190451025214056 ) ) ;
#102332=ORIENTED_EDGE ( 'NONE', *, *, #45209, .T. ) ;
#102334=CARTESIAN_POINT ( 'NONE',  ( 11.68342038867203492, -6.740707523384209310, 11.88629033278121661 ) ) ;
#102336=EDGE_CURVE ( 'NONE', #92516, #75802, #119096, .T. ) ;
#102338=VERTEX_POINT ( 'NONE', #74179 ) ;
#102339=FACE_OUTER_BOUND ( 'NONE', #105618, .T. ) ;
#102340=VERTEX_POINT ( 'NONE', #64725 ) ;
#102341=CARTESIAN_POINT ( 'NONE',  ( -7.499999999999940492, 7.466399257802177836, 5.000000000000000000 ) ) ;
#102342=DIRECTION ( 'NONE',  ( 0.3543493200069162685, -0.000000000000000000, -0.9351131265310288487 ) ) ;
#102344=PLANE ( 'NONE',  #42390 ) ;
#102345=CARTESIAN_POINT ( 'NONE',  ( -21.48921356237309155, -27.52281430457070499, 5.000000000000000000 ) ) ;
#102346=ORIENTED_EDGE ( 'NONE', *, *, #106568, .F. ) ;
#102347=AXIS2_PLACEMENT_3D ( 'NONE', #100672, #34702, #46323 ) ;
#102348=CARTESIAN_POINT ( 'NONE',  ( -14.99999999999988809, 20.96639925780204905, 5.000000000000000000 ) ) ;
#102349=VECTOR ( 'NONE', #112061, 1000.000000000000227 ) ;
#102350=EDGE_CURVE ( 'NONE', #106377, #78830, #7462, .T. ) ;
#102351=VECTOR ( 'NONE', #36855, 1000.000000000000000 ) ;
#102352=DIRECTION ( 'NONE',  ( -0.7071067811865486830, -0.7071067811865464625, -0.000000000000000000 ) ) ;
#102353=CARTESIAN_POINT ( 'NONE',  ( -12.18398860626900060, 28.73617430169795739, 5.000000000000000000 ) ) ;
#102354=EDGE_LOOP ( 'NONE', ( #86759, #103657, #13159 ) ) ;
#102355=PLANE ( 'NONE',  #132307 ) ;
#102356=VECTOR ( 'NONE', #66200, 1000.000000000000114 ) ;
#102357=DIRECTION ( 'NONE',  ( -0.7071067811865486830, -0.7071067811865464625, -0.000000000000000000 ) ) ;
#102359=CARTESIAN_POINT ( 'NONE',  ( -81.18398860626899705, 28.73617430169844056, 5.000000000000000000 ) ) ;
#102360=ORIENTED_EDGE ( 'NONE', *, *, #32505, .T. ) ;
#102361=EDGE_CURVE ( 'NONE', #98488, #113103, #61896, .T. ) ;
#102362=VERTEX_POINT ( 'NONE', #19072 ) ;
#102363=DIRECTION ( 'NONE',  ( -2.781805975412905890E-17, 0.3543493200069152693, 0.9351131265310292928 ) ) ;
#102364=VECTOR ( 'NONE', #45260, 1000.000000000000000 ) ;
#102365=EDGE_LOOP ( 'NONE', ( #38598, #50411, #91947, #137558 ) ) ;
#102368=ORIENTED_EDGE ( 'NONE', *, *, #94737, .F. ) ;
#102369=DIRECTION ( 'NONE',  ( -0.7071067811865487940, 0.7071067811865463515, -0.000000000000000000 ) ) ;
#102370=DIRECTION ( 'NONE',  ( 0.6830127018922180770, -0.6830127018922204085, -0.2588190451025213501 ) ) ;
#102372=CARTESIAN_POINT ( 'NONE',  ( 31.00193056682077142, -22.22500000000000142, 4.500000000000000888 ) ) ;
#102373=CARTESIAN_POINT ( 'NONE',  ( -63.18398860626900415, 28.73617430169831621, 5.000000000000000000 ) ) ;
#102374=AXIS2_PLACEMENT_3D ( 'NONE', #13706, #11560, #12301 ) ;
#102375=LINE ( 'NONE', #58907, #2007 ) ;
#102376=CARTESIAN_POINT ( 'NONE',  ( -2.671830600776452069, 20.25929247661551713, 4.000000000000000000 ) ) ;
#102377=EDGE_CURVE ( 'NONE', #49015, #29472, #63337, .T. ) ;
#102378=DIRECTION ( 'NONE',  ( -0.7071067811865487940, 0.7071067811865463515, -0.000000000000000000 ) ) ;
#102379=ORIENTED_EDGE ( 'NONE', *, *, #110139, .T. ) ;
#102380=ORIENTED_EDGE ( 'NONE', *, *, #54500, .T. ) ;
#102381=ORIENTED_EDGE ( 'NONE', *, *, #112541, .T. ) ;
#102383=EDGE_CURVE ( 'NONE', #34231, #80772, #51725, .T. ) ;
#102384=EDGE_LOOP ( 'NONE', ( #34868, #115626, #124460, #97909 ) ) ;
#102385=ORIENTED_EDGE ( 'NONE', *, *, #44867, .F. ) ;
#102386=VERTEX_POINT ( 'NONE', #40158 ) ;
#102387=VECTOR ( 'NONE', #36197, 1000.000000000000000 ) ;
#102388=CARTESIAN_POINT ( 'NONE',  ( 23.99451991528749062, 28.92564299267954908, 4.000000000000000000 ) ) ;
#102389=CARTESIAN_POINT ( 'NONE',  ( -32.99999999999976552, -19.22509904557639615, 1.855685503482101595 ) ) ;
#102390=ORIENTED_EDGE ( 'NONE', *, *, #101241, .F. ) ;
#102391=FACE_OUTER_BOUND ( 'NONE', #129817, .T. ) ;
#102392=LINE ( 'NONE', #69044, #97619 ) ;
#102394=DIRECTION ( 'NONE',  ( 0.7071067811865487940, 0.7071067811865463515, 0.000000000000000000 ) ) ;
#102397=EDGE_CURVE ( 'NONE', #91589, #100881, #129986, .T. ) ;
#102398=DIRECTION ( 'NONE',  ( -0.3543493200069162685, -0.000000000000000000, -0.9351131265310288487 ) ) ;
#102399=CARTESIAN_POINT ( 'NONE',  ( -66.18398860626901126, 28.73617430169833753, 5.000000000000000000 ) ) ;
#102400=DIRECTION ( 'NONE',  ( 0.7071067811865487940, 0.7071067811865463515, 0.000000000000000000 ) ) ;
#102401=VECTOR ( 'NONE', #44253, 1000.000000000000000 ) ;
#102402=CARTESIAN_POINT ( 'NONE',  ( -26.99451991528749417, 28.92564299267956685, 4.000000000000000000 ) ) ;
#102403=DIRECTION ( 'NONE',  ( -0.7071067811865487940, 0.7071067811865463515, -0.000000000000000000 ) ) ;
#102404=DIRECTION ( 'NONE',  ( -0.000000000000000000, 0.000000000000000000, 1.000000000000000000 ) ) ;
#102405=PLANE ( 'NONE',  #31938 ) ;
#102408=CARTESIAN_POINT ( 'NONE',  ( -56.99451991528749062, 28.92564299267978001, 4.000000000000000000 ) ) ;
#102409=DIRECTION ( 'NONE',  ( -0.3543493200069162685, -0.000000000000000000, -0.9351131265310288487 ) ) ;
#102410=ORIENTED_EDGE ( 'NONE', *, *, #31343, .F. ) ;
#102411=EDGE_LOOP ( 'NONE', ( #103807, #103903, #49915, #67373 ) ) ;
#102414=ORIENTED_EDGE ( 'NONE', *, *, #52725, .T. ) ;
#102415=CARTESIAN_POINT ( 'NONE',  ( -34.92500000000001137, 7.711264365774168184, -0.4997969837368162471 ) ) ;
#102416=CARTESIAN_POINT ( 'NONE',  ( 45.48921356237309510, -27.52281430457087197, 5.000000000000000000 ) ) ;
#102417=VERTEX_POINT ( 'NONE', #117638 ) ;
#102418=VECTOR ( 'NONE', #70985, 999.9999999999998863 ) ;
#102419=AXIS2_PLACEMENT_3D ( 'NONE', #11902, #109076, #77903 ) ;
#102420=VECTOR ( 'NONE', #122364, 1000.000000000000000 ) ;
#102421=CARTESIAN_POINT ( 'NONE',  ( 1.499999999999990896, -19.53360074219753884, 5.000000000000000000 ) ) ;
#102422=CARTESIAN_POINT ( 'NONE',  ( -14.24139925780194105, 21.72500000000000142, 5.000000000000000000 ) ) ;
#102423=VECTOR ( 'NONE', #6154, 1000.000000000000000 ) ;
#102426=ORIENTED_EDGE ( 'NONE', *, *, #53610, .F. ) ;
#102427=LINE ( 'NONE', #2332, #50297 ) ;
#102428=ORIENTED_EDGE ( 'NONE', *, *, #61199, .F. ) ;
#102430=DIRECTION ( 'NONE',  ( -0.000000000000000000, -0.3543493200069152138, 0.9351131265310292928 ) ) ;
#102431=LINE ( 'NONE', #3079, #70895 ) ;
#102433=DIRECTION ( 'NONE',  ( 0.7071067811865487940, -0.7071067811865463515, 0.000000000000000000 ) ) ;
#102434=ORIENTED_EDGE ( 'NONE', *, *, #107169, .F. ) ;
#102435=ORIENTED_EDGE ( 'NONE', *, *, #131399, .T. ) ;
#102437=DIRECTION ( 'NONE',  ( 0.7071067811865486830, -0.7071067811865464625, -0.000000000000000000 ) ) ;
#102438=CARTESIAN_POINT ( 'NONE',  ( -29.29289321881324426, -3.740707523384243505, 5.000000000000000000 ) ) ;
#102439=CARTESIAN_POINT ( 'NONE',  ( -42.18398860626899705, 28.73617430169816700, 5.000000000000000000 ) ) ;
#102440=LINE ( 'NONE', #135762, #127223 ) ;
#102441=EDGE_CURVE ( 'NONE', #125750, #114249, #108188, .T. ) ;
#102443=EDGE_CURVE ( 'NONE', #105448, #75123, #85044, .T. ) ;
#102445=CYLINDRICAL_SURFACE ( 'NONE', #50080, 0.5000000000000004441 ) ;
#102448=VERTEX_POINT ( 'NONE', #8848 ) ;
#102454=ORIENTED_EDGE ( 'NONE', *, *, #1767, .T. ) ;
#102456=CYLINDRICAL_SURFACE ( 'NONE', #21471, 0.5000000000000004441 ) ;
#102457=AXIS2_PLACEMENT_3D ( 'NONE', #81193, #92742, #68895 ) ;
#102458=CARTESIAN_POINT ( 'NONE',  ( -34.42500000000001137, 22.22500000000000142, 4.165035510187088619 ) ) ;
#102459=EDGE_CURVE ( 'NONE', #28383, #36162, #75611, .T. ) ;
#102460=FACE_BOUND ( 'NONE', #75318, .T. ) ;
#102461=ADVANCED_FACE ( 'NONE', ( #9598 ), #34245, .F. ) ;
#102462=DIRECTION ( 'NONE',  ( -0.7071067811865487940, 0.7071067811865463515, -0.000000000000000000 ) ) ;
#102464=CARTESIAN_POINT ( 'NONE',  ( 25.82816939922335564, 0.7592924766157207461, 4.000000000000000000 ) ) ;
#102465=CARTESIAN_POINT ( 'NONE',  ( -20.99999999999984723, -19.06887692260762179, 4.000000000000000000 ) ) ;
#102466=ORIENTED_EDGE ( 'NONE', *, *, #6083, .F. ) ;
#102467=CARTESIAN_POINT ( 'NONE',  ( 23.29289321881329755, -6.740707523384216415, 5.000000000000000000 ) ) ;
#102468=EDGE_CURVE ( 'NONE', #84739, #20850, #77057, .T. ) ;
#102470=ORIENTED_EDGE ( 'NONE', *, *, #32806, .F. ) ;
#102472=ORIENTED_EDGE ( 'NONE', *, *, #121237, .T. ) ;
#102473=DIRECTION ( 'NONE',  ( -0.6830127018922181881, 0.6830127018922202975, -0.2588190451025214056 ) ) ;
#102474=ORIENTED_EDGE ( 'NONE', *, *, #47864, .F. ) ;
#102475=LINE ( 'NONE', #14728, #11984 ) ;
#102478=CARTESIAN_POINT ( 'NONE',  ( 30.78162688292473348, 21.74787736706807095, 4.999607392498048419 ) ) ;
#102479=DIRECTION ( 'NONE',  ( -0.7071067811865487940, 0.7071067811865463515, -0.000000000000000000 ) ) ;
#102480=DIRECTION ( 'NONE',  ( 1.000000000000000000, 0.000000000000000000, 0.000000000000000000 ) ) ;
#102481=LINE ( 'NONE', #36489, #64341 ) ;
#102482=CARTESIAN_POINT ( 'NONE',  ( -10.49999999999992184, -10.53360074219763121, 5.000000000000000000 ) ) ;
#102483=CARTESIAN_POINT ( 'NONE',  ( -14.81601139373099585, 28.73617430169776910, 5.000000000000000000 ) ) ;
#102484=DIRECTION ( 'NONE',  ( 0.7071067811865487940, -0.7071067811865463515, 0.000000000000000000 ) ) ;
#102485=ORIENTED_EDGE ( 'NONE', *, *, #72582, .T. ) ;
#102486=EDGE_CURVE ( 'NONE', #118739, #97187, #12469, .T. ) ;
#102488=VERTEX_POINT ( 'NONE', #112510 ) ;
#102490=LINE ( 'NONE', #47428, #39700 ) ;
#102491=ORIENTED_EDGE ( 'NONE', *, *, #40880, .F. ) ;
#102492=ORIENTED_EDGE ( 'NONE', *, *, #20708, .T. ) ;
#102493=ORIENTED_EDGE ( 'NONE', *, *, #38930, .F. ) ;
#102494=LINE ( 'NONE', #5971, #67021 ) ;
#102496=ORIENTED_EDGE ( 'NONE', *, *, #52460, .F. ) ;
#102499=LINE ( 'NONE', #68459, #14534 ) ;
#102501=DIRECTION ( 'NONE',  ( -0.7071067811865486830, -0.7071067811865464625, 0.000000000000000000 ) ) ;
#102502=VERTEX_POINT ( 'NONE', #133562 ) ;
#102503=DIRECTION ( 'NONE',  ( -0.000000000000000000, -1.000000000000000000, -0.000000000000000000 ) ) ;
#102504=CARTESIAN_POINT ( 'NONE',  ( 33.15612307739218778, -22.22500000000000142, 4.000000000000000000 ) ) ;
#102505=LINE ( 'NONE', #133695, #142400 ) ;
#102506=VECTOR ( 'NONE', #29918, 1000.000000000000227 ) ;
#102507=LINE ( 'NONE', #111194, #30934 ) ;
#102508=ORIENTED_EDGE ( 'NONE', *, *, #61456, .T. ) ;
#102509=AXIS2_PLACEMENT_3D ( 'NONE', #34678, #78912, #57170 ) ;
#102513=VECTOR ( 'NONE', #29730, 1000.000000000000000 ) ;
#102514=FACE_OUTER_BOUND ( 'NONE', #88228, .T. ) ;
#102515=VECTOR ( 'NONE', #32214, 999.9999999999998863 ) ;
#102516=ORIENTED_EDGE ( 'NONE', *, *, #140086, .T. ) ;
#102517=DIRECTION ( 'NONE',  ( -0.7071067811865487940, 0.7071067811865463515, 0.000000000000000000 ) ) ;
#102518=EDGE_CURVE ( 'NONE', #53303, #79366, #133, .T. ) ;
#102520=CARTESIAN_POINT ( 'NONE',  ( 0.6664792200040612347, -22.22500000000000142, 18.48694195581934352 ) ) ;
#102521=FACE_OUTER_BOUND ( 'NONE', #24306, .T. ) ;
#102523=ORIENTED_EDGE ( 'NONE', *, *, #59737, .T. ) ;
#102526=DIRECTION ( 'NONE',  ( -0.7071067811865487940, 0.7071067811865463515, 0.000000000000000000 ) ) ;
#102528=DIRECTION ( 'NONE',  ( 0.7071067811865486830, -0.7071067811865464625, -0.000000000000000000 ) ) ;
#102529=CARTESIAN_POINT ( 'NONE',  ( -22.49999999999983658, 13.46639925780212721, 5.000000000000000000 ) ) ;
#102530=ORIENTED_EDGE ( 'NONE', *, *, #45534, .F. ) ;
#102532=ORIENTED_EDGE ( 'NONE', *, *, #101129, .F. ) ;
#102534=DIRECTION ( 'NONE',  ( 0.7071067811865486830, -0.7071067811865464625, -0.000000000000000000 ) ) ;
#102537=VECTOR ( 'NONE', #29400, 1000.000000000000227 ) ;
#102538=PLANE ( 'NONE',  #43842 ) ;
#102539=CARTESIAN_POINT ( 'NONE',  ( -32.99999999999976552, -4.447814304570784749, 5.000000000000000000 ) ) ;
#102540=CARTESIAN_POINT ( 'NONE',  ( -29.29289321881324781, -12.74070752338415780, 5.000000000000000000 ) ) ;
#102542=CARTESIAN_POINT ( 'NONE',  ( -9.707106781186471522, 5.259292476615662792, 5.000000000000000000 ) ) ;
#102543=DIRECTION ( 'NONE',  ( 0.3543493200069162685, -0.000000000000000000, -0.9351131265310288487 ) ) ;
#102544=DIRECTION ( 'NONE',  ( -0.7071067811865486830, -0.7071067811865464625, 0.000000000000000000 ) ) ;
#102546=VECTOR ( 'NONE', #14390, 1000.000000000000227 ) ;
#102548=PLANE ( 'NONE',  #44208 ) ;
#102549=EDGE_CURVE ( 'NONE', #41843, #56470, #76324, .T. ) ;
#102550=AXIS2_PLACEMENT_3D ( 'NONE', #123577, #80075, #68479 ) ;
#102552=DIRECTION ( 'NONE',  ( 0.7071067811865487940, 0.7071067811865463515, 0.000000000000000000 ) ) ;
#102553=ORIENTED_EDGE ( 'NONE', *, *, #55818, .T. ) ;
#102554=DIRECTION ( 'NONE',  ( -0.7071067811865487940, 0.7071067811865463515, -0.000000000000000000 ) ) ;
#102556=DIRECTION ( 'NONE',  ( -0.7071067811865486830, -0.7071067811865464625, 0.000000000000000000 ) ) ;
#102557=FACE_OUTER_BOUND ( 'NONE', #53066, .T. ) ;
#102558=DIRECTION ( 'NONE',  ( -0.7071067811865486830, -0.7071067811865464625, 0.000000000000000000 ) ) ;
#102559=ADVANCED_FACE ( 'NONE', ( #1567 ), #77756, .F. ) ;
#102560=DIRECTION ( 'NONE',  ( 0.000000000000000000, -1.000000000000000000, 0.000000000000000000 ) ) ;
#102561=DIRECTION ( 'NONE',  ( 0.3543493200069162685, -0.000000000000000000, -0.9351131265310288487 ) ) ;
#102562=ORIENTED_EDGE ( 'NONE', *, *, #117813, .F. ) ;
#102564=EDGE_LOOP ( 'NONE', ( #23967, #57344, #119477, #23472 ) ) ;
#102565=CARTESIAN_POINT ( 'NONE',  ( -6.489213562373093325, -27.52281430457059841, 5.000000000000000000 ) ) ;
#102566=LINE ( 'NONE', #135887, #95455 ) ;
#102568=DIRECTION ( 'NONE',  ( 0.6830127018922180770, -0.6830127018922204085, -0.2588190451025213501 ) ) ;
#102569=DIRECTION ( 'NONE',  ( -0.6830127018922180770, -0.6830127018922202975, -0.2588190451025213501 ) ) ;
#102570=AXIS2_PLACEMENT_3D ( 'NONE', #47134, #60107, #47823 ) ;
#102572=FACE_OUTER_BOUND ( 'NONE', #104621, .T. ) ;
#102573=CARTESIAN_POINT ( 'NONE',  ( 51.18398860626899705, 28.73617430169823095, 5.000000000000000000 ) ) ;
#102574=VERTEX_POINT ( 'NONE', #32836 ) ;
#102576=CARTESIAN_POINT ( 'NONE',  ( 0.005480084712502889671, 28.92564299267938210, 4.000000000000000000 ) ) ;
#102577=CARTESIAN_POINT ( 'NONE',  ( 14.29289321881336150, 11.25929247661560773, 5.000000000000000000 ) ) ;
#102579=VECTOR ( 'NONE', #88189, 1000.000000000000000 ) ;
#102580=VECTOR ( 'NONE', #2491, 999.9999999999998863 ) ;
#102581=ORIENTED_EDGE ( 'NONE', *, *, #111669, .T. ) ;
#102582=ADVANCED_FACE ( 'NONE', ( #24080 ), #23340, .F. ) ;
#102583=DIRECTION ( 'NONE',  ( -0.000000000000000000, 0.000000000000000000, 1.000000000000000000 ) ) ;
#102586=CARTESIAN_POINT ( 'NONE',  ( -72.29974487139158157, -27.71228299555256669, 4.000000000000000000 ) ) ;
#102587=ORIENTED_EDGE ( 'NONE', *, *, #102129, .T. ) ;
#102588=ORIENTED_EDGE ( 'NONE', *, *, #72046, .F. ) ;
#102589=VECTOR ( 'NONE', #25748, 1000.000000000000000 ) ;
#102590=CARTESIAN_POINT ( 'NONE',  ( 32.99451991528749062, 28.92564299267960948, 4.000000000000000000 ) ) ;
#102591=CARTESIAN_POINT ( 'NONE',  ( 22.49999999999985079, -1.912538124160733766, 4.000000000000000000 ) ) ;
#102593=CARTESIAN_POINT ( 'NONE',  ( 1.171830600776468945, 6.759292476615660128, 4.000000000000000000 ) ) ;
#102595=ORIENTED_EDGE ( 'NONE', *, *, #101966, .F. ) ;
#102598=AXIS2_PLACEMENT_3D ( 'NONE', #50679, #28928, #127524 ) ;
#102600=DIRECTION ( 'NONE',  ( -0.7071067811865486830, 0.7071067811865464625, 0.000000000000000000 ) ) ;
#102601=EDGE_LOOP ( 'NONE', ( #105612, #109385, #34570, #14366 ) ) ;
#102604=EDGE_LOOP ( 'NONE', ( #132877, #136340, #73154, #16066, #119553 ) ) ;
#102605=EDGE_CURVE ( 'NONE', #74021, #52888, #22606, .T. ) ;
#102606=DIRECTION ( 'NONE',  ( 0.7071067811865487940, 0.7071067811865463515, 0.000000000000000000 ) ) ;
#102609=ORIENTED_EDGE ( 'NONE', *, *, #31880, .T. ) ;
#102610=EDGE_LOOP ( 'NONE', ( #91971, #93185, #135066, #33650 ) ) ;
#102611=VECTOR ( 'NONE', #118166, 1000.000000000000000 ) ;
#102612=CARTESIAN_POINT ( 'NONE',  ( 0.000000000000000000, 0.000000000000000000, 5.000000000000000000 ) ) ;
#102614=EDGE_CURVE ( 'NONE', #137076, #46388, #121232, .T. ) ;
#102615=EDGE_CURVE ( 'NONE', #115197, #4933, #2277, .T. ) ;
#102617=VERTEX_POINT ( 'NONE', #66171 ) ;
#102620=CARTESIAN_POINT ( 'NONE',  ( -15.29974487139158867, -27.71228299555216879, 4.000000000000000000 ) ) ;
#102621=PLANE ( 'NONE',  #116531 ) ;
#102622=AXIS2_PLACEMENT_3D ( 'NONE', #125682, #95884, #26362 ) ;
#102623=ORIENTED_EDGE ( 'NONE', *, *, #88951, .F. ) ;
#102624=EDGE_CURVE ( 'NONE', #56866, #136190, #46596, .T. ) ;
#102625=FACE_BOUND ( 'NONE', #26701, .T. ) ;
#102626=EDGE_CURVE ( 'NONE', #138219, #107914, #65470, .T. ) ;
#102627=CARTESIAN_POINT ( 'NONE',  ( 9.017348362375173565, 22.22500000000000142, 21.65139844574516914 ) ) ;
#102628=CARTESIAN_POINT ( 'NONE',  ( 21.32816939922337696, -3.740707523384241728, 4.000000000000000000 ) ) ;
#102629=DIRECTION ( 'NONE',  ( -0.7071067811865486830, -0.7071067811865464625, 0.000000000000000000 ) ) ;
#102630=DIRECTION ( 'NONE',  ( 0.7071067811865487940, 0.7071067811865463515, -0.000000000000000000 ) ) ;
#102631=ORIENTED_EDGE ( 'NONE', *, *, #109213, .T. ) ;
#102632=VECTOR ( 'NONE', #74919, 1000.000000000000000 ) ;
#102633=VERTEX_POINT ( 'NONE', #98760 ) ;
#102635=ORIENTED_EDGE ( 'NONE', *, *, #69725, .T. ) ;
#102636=EDGE_CURVE ( 'NONE', #76093, #270, #45156, .T. ) ;
#102637=CARTESIAN_POINT ( 'NONE',  ( 15.48921356237309510, -27.52281430457066236, 5.000000000000000000 ) ) ;
#102638=ORIENTED_EDGE ( 'NONE', *, *, #19515, .T. ) ;
#102639=DIRECTION ( 'NONE',  ( 0.3543493200069163240, -0.000000000000000000, 0.9351131265310288487 ) ) ;
#102641=AXIS2_PLACEMENT_3D ( 'NONE', #59190, #135311, #70768 ) ;
#102642=LINE ( 'NONE', #123690, #94111 ) ;
#102643=CARTESIAN_POINT ( 'NONE',  ( -22.49999999999984368, -13.53360074219759746, 5.000000000000000000 ) ) ;
#102644=ORIENTED_EDGE ( 'NONE', *, *, #23951, .F. ) ;
#102645=FACE_OUTER_BOUND ( 'NONE', #19435, .T. ) ;
#102646=FACE_OUTER_BOUND ( 'NONE', #114744, .T. ) ;
#102647=VECTOR ( 'NONE', #80761, 1000.000000000000000 ) ;
#102649=CARTESIAN_POINT ( 'NONE',  ( 41.99451991528749062, 28.92564299267967343, 4.000000000000000000 ) ) ;
#102650=FACE_OUTER_BOUND ( 'NONE', #40426, .T. ) ;
#102651=ADVANCED_FACE ( 'NONE', ( #103068 ), #61040, .T. ) ;
#102652=DIRECTION ( 'NONE',  ( 0.3543493200069162685, -0.000000000000000000, -0.9351131265310288487 ) ) ;
#102653=VERTEX_POINT ( 'NONE', #102372 ) ;
#102654=CARTESIAN_POINT ( 'NONE',  ( 0.2997448713915885632, -27.71228299555206220, 4.000000000000000000 ) ) ;
#102655=CARTESIAN_POINT ( 'NONE',  ( -6.299744871391586898, -27.71228299555210484, 4.000000000000000000 ) ) ;
#102656=VECTOR ( 'NONE', #113527, 1000.000000000000227 ) ;
#102657=ORIENTED_EDGE ( 'NONE', *, *, #57353, .F. ) ;
#102658=ORIENTED_EDGE ( 'NONE', *, *, #71691, .T. ) ;
#102659=ORIENTED_EDGE ( 'NONE', *, *, #71521, .F. ) ;
#102662=EDGE_CURVE ( 'NONE', #134058, #118870, #47995, .T. ) ;
#102663=VERTEX_POINT ( 'NONE', #137125 ) ;
#102664=EDGE_CURVE ( 'NONE', #35075, #135973, #126248, .T. ) ;
#102666=( BOUNDED_CURVE ( )  B_SPLINE_CURVE ( 3, ( #30188, #128105, #83902, #95445 ),
 .UNSPECIFIED., .F., .T. ) 
 B_SPLINE_CURVE_WITH_KNOTS ( ( 4, 4 ),
 ( 5.143245962375964986, 6.645403452391246191 ),
 .UNSPECIFIED. ) 
 CURVE ( )  GEOMETRIC_REPRESENTATION_ITEM ( )  RATIONAL_B_SPLINE_CURVE ( ( 1.000000000000000000, 0.8206354192515240564, 0.8206354192515240564, 1.000000000000000000 ) ) 
 REPRESENTATION_ITEM ( '' )  );
#102667=LINE ( 'NONE', #46159, #77268 ) ;
#102668=EDGE_LOOP ( 'NONE', ( #43982, #126571, #123202, #123406 ) ) ;
#102669=CARTESIAN_POINT ( 'NONE',  ( 3.299744871391591339, -27.71228299555208352, 4.000000000000000000 ) ) ;
#102670=ORIENTED_EDGE ( 'NONE', *, *, #54339, .T. ) ;
#102671=DIRECTION ( 'NONE',  ( 0.7071067811865487940, -0.7071067811865463515, 0.000000000000000000 ) ) ;
#102673=CARTESIAN_POINT ( 'NONE',  ( -33.79289321881321229, 12.75929247661558641, 5.000000000000000000 ) ) ;
#102675=ORIENTED_EDGE ( 'NONE', *, *, #56518, .F. ) ;
#102676=CARTESIAN_POINT ( 'NONE',  ( 10.49999999999992895, 3.653845994658403651, -4.504631822206392577 ) ) ;
#102678=CARTESIAN_POINT ( 'NONE',  ( -1.069960254864079419, -0.7407075233842770334, 13.87443053587611175 ) ) ;
#102679=ORIENTED_EDGE ( 'NONE', *, *, #86316, .T. ) ;
#102680=LINE ( 'NONE', #12775, #6422 ) ;
#102681=EDGE_LOOP ( 'NONE', ( #28872, #2626, #42667, #34485 ) ) ;
#102682=ORIENTED_EDGE ( 'NONE', *, *, #133759, .F. ) ;
#102683=EDGE_LOOP ( 'NONE', ( #103449, #94179, #80560, #40554, #135588 ) ) ;
#102684=FACE_OUTER_BOUND ( 'NONE', #102082, .T. ) ;
#102685=VECTOR ( 'NONE', #92893, 1000.000000000000000 ) ;
#102687=DIRECTION ( 'NONE',  ( -0.7071067811865487940, 0.7071067811865463515, 0.000000000000000000 ) ) ;
#102688=LINE ( 'NONE', #14230, #44037 ) ;
#102689=CARTESIAN_POINT ( 'NONE',  ( 33.48921356237309510, -27.52281430457078670, 5.000000000000000000 ) ) ;
#102690=ORIENTED_EDGE ( 'NONE', *, *, #96349, .T. ) ;
#102693=DIRECTION ( 'NONE',  ( 0.7071067811865487940, 0.7071067811865463515, 0.000000000000000000 ) ) ;
#102694=LINE ( 'NONE', #22936, #57627 ) ;
#102695=DIRECTION ( 'NONE',  ( -0.7071067811865486830, -0.7071067811865464625, 0.000000000000000000 ) ) ;
#102696=EDGE_LOOP ( 'NONE', ( #74752, #50323, #51866, #25476 ) ) ;
#102698=ADVANCED_FACE ( 'NONE', ( #15300 ), #125545, .F. ) ;
#102699=ORIENTED_EDGE ( 'NONE', *, *, #74466, .T. ) ;
#102702=DIRECTION ( 'NONE',  ( 0.3543493200069162685, -0.000000000000000000, -0.9351131265310288487 ) ) ;
#102705=FACE_OUTER_BOUND ( 'NONE', #27708, .T. ) ;
#102707=CARTESIAN_POINT ( 'NONE',  ( 12.75860074219786711, 21.72500000000000142, 5.000000000000000000 ) ) ;
#102708=CARTESIAN_POINT ( 'NONE',  ( -8.999999999999937828, 7.007997736742436423, -8.085015511992134307 ) ) ;
#102709=DIRECTION ( 'NONE',  ( -0.7071067811865487940, 0.7071067811865463515, -0.000000000000000000 ) ) ;
#102711=VERTEX_POINT ( 'NONE', #4387 ) ;
#102712=CARTESIAN_POINT ( 'NONE',  ( 6.302772524220206840, -22.22500000000000142, -10.62274418449467284 ) ) ;
#102713=ORIENTED_EDGE ( 'NONE', *, *, #32210, .F. ) ;
#102717=ADVANCED_FACE ( 'NONE', ( #48688 ), #92892, .F. ) ;
#102719=LINE ( 'NONE', #6203, #130624 ) ;
#102720=ORIENTED_EDGE ( 'NONE', *, *, #49271, .F. ) ;
#102721=EDGE_CURVE ( 'NONE', #102268, #115069, #113934, .T. ) ;
#102723=ORIENTED_EDGE ( 'NONE', *, *, #57982, .F. ) ;
#102726=CARTESIAN_POINT ( 'NONE',  ( -2.999999999999981792, 8.966399257802175171, 5.000000000000000000 ) ) ;
#102728=CARTESIAN_POINT ( 'NONE',  ( -27.48921356237309155, -27.52281430457074762, 5.000000000000000000 ) ) ;
#102731=ORIENTED_EDGE ( 'NONE', *, *, #129943, .T. ) ;
#102732=EDGE_CURVE ( 'NONE', #74042, #99982, #69026, .T. ) ;
#102733=DIRECTION ( 'NONE',  ( -0.000000000000000000, 0.3543493200069153248, 0.9351131265310292928 ) ) ;
#102734=CARTESIAN_POINT ( 'NONE',  ( 30.48921356237309510, -27.52281430457076894, 5.000000000000000000 ) ) ;
#102735=LINE ( 'NONE', #123787, #143318 ) ;
#102737=CARTESIAN_POINT ( 'NONE',  ( 6.489213562373093325, -27.52281430457059841, 5.000000000000000000 ) ) ;
#102738=LINE ( 'NONE', #114310, #9581 ) ;
#102739=ORIENTED_EDGE ( 'NONE', *, *, #67966, .F. ) ;
#102740=VECTOR ( 'NONE', #110305, 1000.000000000000227 ) ;
#102741=EDGE_CURVE ( 'NONE', #39763, #99698, #82065, .T. ) ;
#102744=VECTOR ( 'NONE', #108161, 1000.000000000000227 ) ;
#102746=CARTESIAN_POINT ( 'NONE',  ( -3.299744871391591339, -27.71228299555208352, 4.000000000000000000 ) ) ;
#102747=CYLINDRICAL_SURFACE ( 'NONE', #53250, 0.5000000000000004441 ) ;
#102750=ORIENTED_EDGE ( 'NONE', *, *, #105471, .T. ) ;
#102751=EDGE_CURVE ( 'NONE', #77866, #102292, #135698, .T. ) ;
#102752=CARTESIAN_POINT ( 'NONE',  ( -34.92500000000001137, -13.29806943317885448, 4.500000000000000888 ) ) ;
#102753=AXIS2_PLACEMENT_3D ( 'NONE', #72792, #116945, #43674 ) ;
#102755=ORIENTED_EDGE ( 'NONE', *, *, #130646, .T. ) ;
#102757=FACE_OUTER_BOUND ( 'NONE', #36332, .T. ) ;
#102758=CARTESIAN_POINT ( 'NONE',  ( -34.75611968250420603, -1.294349301475922642, 4.955485411084897152 ) ) ;
#102759=ORIENTED_EDGE ( 'NONE', *, *, #79321, .F. ) ;
#102760=DIRECTION ( 'NONE',  ( -0.000000000000000000, -0.3543493200069152693, 0.9351131265310292928 ) ) ;
#102761=EDGE_CURVE ( 'NONE', #66673, #69645, #29072, .T. ) ;
#102763=DIRECTION ( 'NONE',  ( 0.7071067811865486830, -0.7071067811865464625, -0.000000000000000000 ) ) ;
#102764=VECTOR ( 'NONE', #77410, 999.9999999999998863 ) ;
#102765=PLANE ( 'NONE',  #116402 ) ;
#102766=VECTOR ( 'NONE', #47763, 1000.000000000000227 ) ;
#102767=VERTEX_POINT ( 'NONE', #31226 ) ;
#102769=VERTEX_POINT ( 'NONE', #74743 ) ;
#102771=VECTOR ( 'NONE', #5632, 1000.000000000000000 ) ;
#102772=VERTEX_POINT ( 'NONE', #19613 ) ;
#102774=EDGE_CURVE ( 'NONE', #134932, #46795, #105884, .T. ) ;
#102775=CARTESIAN_POINT ( 'NONE',  ( 15.18398860626900237, 28.73617430169797871, 5.000000000000000000 ) ) ;
#102776=AXIS2_PLACEMENT_3D ( 'NONE', #101274, #1222, #55650 ) ;
#102777=CARTESIAN_POINT ( 'NONE',  ( 27.48921356237309155, -27.52281430457074762, 5.000000000000000000 ) ) ;
#102778=DIRECTION ( 'NONE',  ( -0.7071067811865487940, 0.7071067811865463515, -0.000000000000000000 ) ) ;
#102779=ORIENTED_EDGE ( 'NONE', *, *, #43583, .T. ) ;
#102781=LINE ( 'NONE', #2725, #49022 ) ;
#102782=EDGE_CURVE ( 'NONE', #75896, #68092, #64551, .T. ) ;
#102783=EDGE_CURVE ( 'NONE', #78277, #24426, #6546, .T. ) ;
#102784=CARTESIAN_POINT ( 'NONE',  ( 28.00193056682079273, -22.22500000000000142, 4.500000000000000888 ) ) ;
#102786=ORIENTED_EDGE ( 'NONE', *, *, #41876, .F. ) ;
#102787=CARTESIAN_POINT ( 'NONE',  ( 14.50183651486034364, -17.24070752338410628, 8.407044977365188743 ) ) ;
#102789=AXIS2_PLACEMENT_3D ( 'NONE', #40984, #84505, #117090 ) ;
#102790=CARTESIAN_POINT ( 'NONE',  ( -18.29974487139159223, -27.71228299555219010, 4.000000000000000000 ) ) ;
#102794=PLANE ( 'NONE',  #35361 ) ;
#102795=EDGE_CURVE ( 'NONE', #108674, #11065, #118924, .T. ) ;
#102796=EDGE_CURVE ( 'NONE', #65481, #31173, #107255, .T. ) ;
#102799=LINE ( 'NONE', #91894, #95131 ) ;
#102800=PLANE ( 'NONE',  #37236 ) ;
#102801=LINE ( 'NONE', #88358, #140028 ) ;
#102802=VECTOR ( 'NONE', #59712, 1000.000000000000000 ) ;
#102803=ORIENTED_EDGE ( 'NONE', *, *, #117526, .T. ) ;
#102804=ORIENTED_EDGE ( 'NONE', *, *, #83176, .F. ) ;
#102805=EDGE_CURVE ( 'NONE', #33459, #54679, #106589, .T. ) ;
#102806=DIRECTION ( 'NONE',  ( -0.6830127018922180770, -0.6830127018922204085, -0.2588190451025213501 ) ) ;
#102807=ORIENTED_EDGE ( 'NONE', *, *, #75384, .F. ) ;
#102808=EDGE_CURVE ( 'NONE', #67882, #118195, #29761, .T. ) ;
#102809=AXIS2_PLACEMENT_3D ( 'NONE', #110616, #133143, #93003 ) ;
#102811=VERTEX_POINT ( 'NONE', #96425 ) ;
#102812=DIRECTION ( 'NONE',  ( -0.000000000000000000, 0.000000000000000000, 1.000000000000000000 ) ) ;
#102813=CARTESIAN_POINT ( 'NONE',  ( 32.99451991528749062, 28.92564299267960948, 4.000000000000000000 ) ) ;
#102814=DIRECTION ( 'NONE',  ( -0.6830127018922181881, 0.6830127018922202975, -0.2588190451025214056 ) ) ;
#102816=LINE ( 'NONE', #3458, #63029 ) ;
#102817=EDGE_LOOP ( 'NONE', ( #82559, #140967, #58770, #91315 ) ) ;
#102818=LINE ( 'NONE', #3460, #61070 ) ;
#102820=ORIENTED_EDGE ( 'NONE', *, *, #101647, .T. ) ;
#102822=ORIENTED_EDGE ( 'NONE', *, *, #21103, .T. ) ;
#102823=ORIENTED_EDGE ( 'NONE', *, *, #52871, .T. ) ;
#102824=LINE ( 'NONE', #3466, #52825 ) ;
#102825=ORIENTED_EDGE ( 'NONE', *, *, #113747, .T. ) ;
#102826=ORIENTED_EDGE ( 'NONE', *, *, #94202, .F. ) ;
#102827=PLANE ( 'NONE',  #39498 ) ;
#102828=VECTOR ( 'NONE', #121348, 1000.000000000000000 ) ;
#102829=EDGE_LOOP ( 'NONE', ( #35451, #71956, #25501, #7597 ) ) ;
#102830=EDGE_CURVE ( 'NONE', #127404, #94791, #30509, .T. ) ;
#102831=DIRECTION ( 'NONE',  ( 0.7071067811865486830, -0.7071067811865464625, -0.000000000000000000 ) ) ;
#102833=AXIS2_PLACEMENT_3D ( 'NONE', #98097, #95223, #30717 ) ;
#102834=CARTESIAN_POINT ( 'NONE',  ( 45.48921356237309510, -27.52281430457087197, 5.000000000000000000 ) ) ;
#102836=CARTESIAN_POINT ( 'NONE',  ( -39.51168605928408084, 6.759292476615653023, 16.35960578974478707 ) ) ;
#102837=EDGE_CURVE ( 'NONE', #137801, #70973, #86322, .T. ) ;
#102838=LINE ( 'NONE', #2036, #124610 ) ;
#102839=LINE ( 'NONE', #52018, #16547 ) ;
#102841=EDGE_CURVE ( 'NONE', #108986, #114269, #95748, .T. ) ;
#102842=CARTESIAN_POINT ( 'NONE',  ( -34.92500000000001137, 22.22500000000000142, 4.000000000000000000 ) ) ;
#102844=ORIENTED_EDGE ( 'NONE', *, *, #48686, .T. ) ;
#102845=FACE_OUTER_BOUND ( 'NONE', #68188, .T. ) ;
#102846=VECTOR ( 'NONE', #79739, 1000.000000000000000 ) ;
#102848=ORIENTED_EDGE ( 'NONE', *, *, #25938, .F. ) ;
#102849=ORIENTED_EDGE ( 'NONE', *, *, #9549, .T. ) ;
#102850=FACE_OUTER_BOUND ( 'NONE', #53561, .T. ) ;
#102851=ORIENTED_EDGE ( 'NONE', *, *, #118777, .F. ) ;
#102852=CARTESIAN_POINT ( 'NONE',  ( 22.17183060077632817, 15.75929247661557042, 4.000000000000000000 ) ) ;
#102855=AXIS2_PLACEMENT_3D ( 'NONE', #113169, #94, #57404 ) ;
#102856=CARTESIAN_POINT ( 'NONE',  ( -63.29974487139158867, -27.71228299555250274, 4.000000000000000000 ) ) ;
#102858=ORIENTED_EDGE ( 'NONE', *, *, #76639, .T. ) ;
#102859=PLANE ( 'NONE',  #83556 ) ;
#102860=ORIENTED_EDGE ( 'NONE', *, *, #31773, .T. ) ;
#102861=CARTESIAN_POINT ( 'NONE',  ( -16.46004848586580493, -22.22500000000000142, -1.997060384840000369 ) ) ;
#102862=VECTOR ( 'NONE', #93573, 1000.000000000000000 ) ;
#102863=AXIS2_PLACEMENT_3D ( 'NONE', #3837, #138706, #37232 ) ;
#102865=ORIENTED_EDGE ( 'NONE', *, *, #91631, .F. ) ;
#102867=CARTESIAN_POINT ( 'NONE',  ( -34.49999999999975842, -5.945670655168998842, 4.994342998332166772 ) ) ;
#102868=ORIENTED_EDGE ( 'NONE', *, *, #33163, .T. ) ;
#102869=VERTEX_POINT ( 'NONE', #28370 ) ;
#102870=ORIENTED_EDGE ( 'NONE', *, *, #129155, .T. ) ;
#102871=CARTESIAN_POINT ( 'NONE',  ( 8.816011393731004731, 28.73617430169781173, 5.000000000000000000 ) ) ;
#102872=CARTESIAN_POINT ( 'NONE',  ( 2.207106781186534139, 6.759292476615653023, 5.000000000000000000 ) ) ;
#102873=DIRECTION ( 'NONE',  ( 1.000000000000000000, 0.000000000000000000, 0.000000000000000000 ) ) ;
#102874=FACE_OUTER_BOUND ( 'NONE', #59870, .T. ) ;
#102876=DIRECTION ( 'NONE',  ( -0.000000000000000000, -0.3543493200069152693, 0.9351131265310292928 ) ) ;
#102877=DIRECTION ( 'NONE',  ( -0.7071067811865486830, -0.7071067811865464625, -0.000000000000000000 ) ) ;
#102878=VECTOR ( 'NONE', #109762, 1000.000000000000227 ) ;
#102879=FACE_OUTER_BOUND ( 'NONE', #121018, .T. ) ;
#102880=DIRECTION ( 'NONE',  ( 1.000000000000000000, 0.000000000000000000, 0.000000000000000000 ) ) ;
#102883=ORIENTED_EDGE ( 'NONE', *, *, #124042, .T. ) ;
#102884=ADVANCED_FACE ( 'NONE', ( #72628 ), #129084, .F. ) ;
#102886=ORIENTED_EDGE ( 'NONE', *, *, #50354, .F. ) ;
#102887=EDGE_CURVE ( 'NONE', #10395, #13638, #118185, .T. ) ;
#102889=CARTESIAN_POINT ( 'NONE',  ( 34.42499999999998295, 21.72500000000000142, 4.000000000000000000 ) ) ;
#102890=DIRECTION ( 'NONE',  ( 0.7071067811865486830, -0.7071067811865464625, -0.000000000000000000 ) ) ;
#102891=VERTEX_POINT ( 'NONE', #54423 ) ;
#102893=UNCERTAINTY_MEASURE_WITH_UNIT (LENGTH_MEASURE( 1.000000000000000082E-05 ), #116752, 'distance_accuracy_value', 'NONE');
#102894=VERTEX_POINT ( 'NONE', #10850 ) ;
#102895=EDGE_CURVE ( 'NONE', #74472, #126742, #31927, .T. ) ;
#102896=EDGE_CURVE ( 'NONE', #88917, #3869, #53697, .T. ) ;
#102897=LINE ( 'NONE', #14450, #135551 ) ;
#102898=LINE ( 'NONE', #100746, #80950 ) ;
#102899=CARTESIAN_POINT ( 'NONE',  ( -42.18398860626899705, 28.73617430169816700, 5.000000000000000000 ) ) ;
#102900=DIRECTION ( 'NONE',  ( -0.000000000000000000, -0.3543493200069152693, 0.9351131265310292928 ) ) ;
#102901=CARTESIAN_POINT ( 'NONE',  ( -30.51665438641024153, 22.22500000000000142, 4.500000000000000888 ) ) ;
#102902=EDGE_CURVE ( 'NONE', #108896, #85524, #32653, .T. ) ;
#102903=DIRECTION ( 'NONE',  ( -4.681814790819591790E-17, -0.3543493200069152693, 0.9351131265310292928 ) ) ;
#102904=DIRECTION ( 'NONE',  ( -0.7071067811865487940, 0.7071067811865463515, -0.000000000000000000 ) ) ;
#102906=CARTESIAN_POINT ( 'NONE',  ( -6.792893218813400580, -20.24070752338406720, 5.000000000000000000 ) ) ;
#102907=DIRECTION ( 'NONE',  ( 1.000000000000000000, 0.000000000000000000, 0.000000000000000000 ) ) ;
#102908=PLANE ( 'NONE',  #83743 ) ;
#102909=DIRECTION ( 'NONE',  ( -0.6830127018922180770, -0.6830127018922204085, -0.2588190451025213501 ) ) ;
#102910=ORIENTED_EDGE ( 'NONE', *, *, #36850, .T. ) ;
#102912=EDGE_LOOP ( 'NONE', ( #127011, #77828, #124269, #112752 ) ) ;
#102914=EDGE_CURVE ( 'NONE', #114916, #100722, #143537, .T. ) ;
#102915=EDGE_LOOP ( 'NONE', ( #14083, #3927, #92035, #116886, #68084, #65239 ) ) ;
#102918=CARTESIAN_POINT ( 'NONE',  ( -31.62823445044366011, -8.240707523384200428, 11.38925528200759985 ) ) ;
#102920=ORIENTED_EDGE ( 'NONE', *, *, #3894, .T. ) ;
#102921=ADVANCED_FACE ( 'NONE', ( #11561 ), #700, .F. ) ;
#102922=CARTESIAN_POINT ( 'NONE',  ( 23.99999999999983302, -9.033600742197648970, 5.000000000000000000 ) ) ;
#102923=DIRECTION ( 'NONE',  ( -0.7071067811865486830, 0.7071067811865464625, 0.000000000000000000 ) ) ;
#102924=DIRECTION ( 'NONE',  ( 0.000000000000000000, 1.000000000000000000, 0.000000000000000000 ) ) ;
#102926=FACE_OUTER_BOUND ( 'NONE', #62724, .T. ) ;
#102928=VECTOR ( 'NONE', #24892, 1000.000000000000114 ) ;
#102929=EDGE_CURVE ( 'NONE', #100675, #136109, #123241, .T. ) ;
#102930=CARTESIAN_POINT ( 'NONE',  ( -29.99999999999979039, -10.77435723561697856, -9.972017380717161927 ) ) ;
#102931=CARTESIAN_POINT ( 'NONE',  ( -31.49999999999977973, -1.533600742197726463, 5.000000000000000000 ) ) ;
#102932=DIRECTION ( 'NONE',  ( 0.7071067811865486830, -0.7071067811865464625, -0.000000000000000000 ) ) ;
#102935=VECTOR ( 'NONE', #79792, 999.9999999999998863 ) ;
#102937=ORIENTED_EDGE ( 'NONE', *, *, #95459, .T. ) ;
#102939=VERTEX_POINT ( 'NONE', #120315 ) ;
#102941=EDGE_CURVE ( 'NONE', #70528, #14309, #131236, .T. ) ;
#102942=PLANE ( 'NONE',  #59460 ) ;
#102943=ORIENTED_EDGE ( 'NONE', *, *, #116243, .F. ) ;
#102944=LINE ( 'NONE', #3589, #18943 ) ;
#102946=( BOUNDED_CURVE ( )  B_SPLINE_CURVE ( 3, ( #126842, #27531, #71795, #16666 ),
 .UNSPECIFIED., .F., .F. ) 
 B_SPLINE_CURVE_WITH_KNOTS ( ( 4, 4 ),
 ( 2.431655599645420551, 2.488862747797045305 ),
 .UNSPECIFIED. ) 
 CURVE ( )  GEOMETRIC_REPRESENTATION_ITEM ( )  RATIONAL_B_SPLINE_CURVE ( ( 1.000000000000000000, 0.9997272971104411710, 0.9997272971104411710, 1.000000000000000000 ) ) 
 REPRESENTATION_ITEM ( '' )  );
#102947=EDGE_CURVE ( 'NONE', #130461, #11776, #133397, .T. ) ;
#102949=AXIS2_PLACEMENT_3D ( 'NONE', #116057, #137116, #70480 ) ;
#102951=EDGE_CURVE ( 'NONE', #94040, #49508, #12302, .T. ) ;
#102952=ORIENTED_EDGE ( 'NONE', *, *, #35415, .T. ) ;
#102953=LINE ( 'NONE', #126132, #3626 ) ;
#102954=FACE_OUTER_BOUND ( 'NONE', #105311, .T. ) ;
#102955=( BOUNDED_CURVE ( )  B_SPLINE_CURVE ( 3, ( #57672, #2511, #135231, #80139 ),
 .UNSPECIFIED., .F., .T. ) 
 B_SPLINE_CURVE_WITH_KNOTS ( ( 4, 4 ),
 ( 3.953918675577642539, 4.014082184732835401 ),
 .UNSPECIFIED. ) 
 CURVE ( )  GEOMETRIC_REPRESENTATION_ITEM ( )  RATIONAL_B_SPLINE_CURVE ( ( 1.000000000000000000, 0.9996983854260930169, 0.9996983854260930169, 1.000000000000000000 ) ) 
 REPRESENTATION_ITEM ( '' )  );
#102956=EDGE_CURVE ( 'NONE', #55852, #117536, #91155, .T. ) ;
#102957=ORIENTED_EDGE ( 'NONE', *, *, #116761, .F. ) ;
#102958=ORIENTED_EDGE ( 'NONE', *, *, #126516, .T. ) ;
#102959=VERTEX_POINT ( 'NONE', #22443 ) ;
#102960=DIRECTION ( 'NONE',  ( 0.7071067811865486830, -0.7071067811865464625, -0.000000000000000000 ) ) ;
#102961=DIRECTION ( 'NONE',  ( 0.7071067811865487940, 0.7071067811865463515, 0.000000000000000000 ) ) ;
#102962=AXIS2_PLACEMENT_3D ( 'NONE', #67086, #123631, #24285 ) ;
#102964=VECTOR ( 'NONE', #3511, 999.9999999999998863 ) ;
#102965=DIRECTION ( 'NONE',  ( 0.7071067811865486830, -0.7071067811865464625, -0.000000000000000000 ) ) ;
#102967=VERTEX_POINT ( 'NONE', #122481 ) ;
#102968=EDGE_CURVE ( 'NONE', #37148, #73565, #42823, .T. ) ;
#102969=LINE ( 'NONE', #38422, #126620 ) ;
#102970=ORIENTED_EDGE ( 'NONE', *, *, #24004, .F. ) ;
#102971=ORIENTED_EDGE ( 'NONE', *, *, #58023, .F. ) ;
#102972=CARTESIAN_POINT ( 'NONE',  ( -10.26506670282044453, 12.75929247661558996, 18.34774599283958807 ) ) ;
#102973=DIRECTION ( 'NONE',  ( -0.6830127018922180770, -0.6830127018922204085, -0.2588190451025213501 ) ) ;
#102974=LINE ( 'NONE', #37727, #123014 ) ;
#102975=EDGE_CURVE ( 'NONE', #46538, #142384, #88465, .T. ) ;
#102976=EDGE_LOOP ( 'NONE', ( #18164, #116220, #11553, #44290 ) ) ;
#102977=CARTESIAN_POINT ( 'NONE',  ( 18.18398860626898994, 28.73617430169800002, 5.000000000000000000 ) ) ;
#102979=ADVANCED_FACE ( 'NONE', ( #109484 ), #77597, .F. ) ;
#102980=FACE_BOUND ( 'NONE', #137736, .T. ) ;
#102981=ORIENTED_EDGE ( 'NONE', *, *, #35545, .T. ) ;
#102982=CARTESIAN_POINT ( 'NONE',  ( -8.510786437626906675, -27.52281430457049183, 5.000000000000000000 ) ) ;
#102983=DIRECTION ( 'NONE',  ( -0.7071067811865487940, 0.7071067811865463515, 0.000000000000000000 ) ) ;
#102984=CARTESIAN_POINT ( 'NONE',  ( 5.700255128608413102, -27.71228299555201957, 4.000000000000000000 ) ) ;
#102986=FACE_OUTER_BOUND ( 'NONE', #47942, .T. ) ;
#102988=ORIENTED_EDGE ( 'NONE', *, *, #1398, .F. ) ;
#102989=ORIENTED_EDGE ( 'NONE', *, *, #23332, .T. ) ;
#102990=EDGE_CURVE ( 'NONE', #15277, #111034, #67434, .T. ) ;
#102992=ORIENTED_EDGE ( 'NONE', *, *, #1248, .T. ) ;
#102993=FACE_OUTER_BOUND ( 'NONE', #90787, .T. ) ;
#102994=PLANE ( 'NONE',  #2081 ) ;
#102995=CARTESIAN_POINT ( 'NONE',  ( -0.1839886062690032631, 28.73617430169787568, 5.000000000000000000 ) ) ;
#102997=DIRECTION ( 'NONE',  ( -0.000000000000000000, -0.3543493200069152693, 0.9351131265310292928 ) ) ;
#102999=VECTOR ( 'NONE', #41128, 1000.000000000000000 ) ;
#103000=DIRECTION ( 'NONE',  ( -0.7071067811865486830, -0.7071067811865464625, 0.000000000000000000 ) ) ;
#103001=EDGE_CURVE ( 'NONE', #139983, #32917, #43513, .T. ) ;
#103002=CARTESIAN_POINT ( 'NONE',  ( 63.18398860626900415, 28.73617430169831621, 5.000000000000000000 ) ) ;
#103003=CARTESIAN_POINT ( 'NONE',  ( 26.20710678118636494, -14.24070752338413293, 5.000000000000000000 ) ) ;
#103005=DIRECTION ( 'NONE',  ( 0.6830127018922181881, 0.6830127018922202975, -0.2588190451025214056 ) ) ;
#103006=ORIENTED_EDGE ( 'NONE', *, *, #55281, .F. ) ;
#103007=VERTEX_POINT ( 'NONE', #87734 ) ;
#103008=ORIENTED_EDGE ( 'NONE', *, *, #38759, .F. ) ;
#103009=ORIENTED_EDGE ( 'NONE', *, *, #114729, .T. ) ;
#103011=VERTEX_POINT ( 'NONE', #34086 ) ;
#103012=ORIENTED_EDGE ( 'NONE', *, *, #96182, .T. ) ;
#103013=DIRECTION ( 'NONE',  ( 0.6830127018922181881, 0.6830127018922202975, -0.2588190451025214056 ) ) ;
#103014=DIRECTION ( 'NONE',  ( 0.7071067811865487940, -0.7071067811865463515, 0.000000000000000000 ) ) ;
#103015=ADVANCED_FACE ( 'NONE', ( #110177 ), #66702, .F. ) ;
#103017=ORIENTED_EDGE ( 'NONE', *, *, #33578, .T. ) ;
#103018=FACE_OUTER_BOUND ( 'NONE', #30847, .T. ) ;
#103019=EDGE_LOOP ( 'NONE', ( #120037, #3098, #97234, #86347, #84584 ) ) ;
#103020=DIRECTION ( 'NONE',  ( 0.3543493200069162685, -0.000000000000000000, -0.9351131265310288487 ) ) ;
#103022=CARTESIAN_POINT ( 'NONE',  ( -3.707106781186510602, 14.25929247661557753, 5.000000000000000000 ) ) ;
#103024=VERTEX_POINT ( 'NONE', #136945 ) ;
#103026=CARTESIAN_POINT ( 'NONE',  ( 31.17183060077625356, 15.75929247661555088, 4.000000000000000000 ) ) ;
#103027=VECTOR ( 'NONE', #42676, 1000.000000000000000 ) ;
#103028=DIRECTION ( 'NONE',  ( 0.7071067811865486830, -0.7071067811865464625, -0.000000000000000000 ) ) ;
#103029=DIRECTION ( 'NONE',  ( 1.000000000000000000, 0.000000000000000000, 0.000000000000000000 ) ) ;
#103030=ORIENTED_EDGE ( 'NONE', *, *, #16087, .F. ) ;
#103031=VERTEX_POINT ( 'NONE', #115151 ) ;
#103032=CARTESIAN_POINT ( 'NONE',  ( -23.99451991528749062, 28.92564299267954908, 4.000000000000000000 ) ) ;
#103033=EDGE_LOOP ( 'NONE', ( #94151, #69362, #75897, #122763 ) ) ;
#103035=FACE_OUTER_BOUND ( 'NONE', #48175, .T. ) ;
#103037=DIRECTION ( 'NONE',  ( -0.7071067811865486830, 0.7071067811865464625, 0.000000000000000000 ) ) ;
#103039=ORIENTED_EDGE ( 'NONE', *, *, #114794, .T. ) ;
#103042=LINE ( 'NONE', #94292, #125560 ) ;
#103043=EDGE_LOOP ( 'NONE', ( #8607, #19041, #36922, #26327 ) ) ;
#103044=CARTESIAN_POINT ( 'NONE',  ( 34.92499999999999005, 16.51246187583931402, 4.000000000000000000 ) ) ;
#103045=DIRECTION ( 'NONE',  ( -0.000000000000000000, -0.3543493200069152693, 0.9351131265310292928 ) ) ;
#103046=ADVANCED_FACE ( 'NONE', ( #123950 ), #38355, .F. ) ;
#103048=LINE ( 'NONE', #113190, #97290 ) ;
#103050=ADVANCED_FACE ( 'NONE', ( #103582 ), #126763, .F. ) ;
#103051=ORIENTED_EDGE ( 'NONE', *, *, #142978, .F. ) ;
#103052=DIRECTION ( 'NONE',  ( 0.7071067811865487940, 0.7071067811865463515, -0.000000000000000000 ) ) ;
#103053=FACE_OUTER_BOUND ( 'NONE', #18042, .T. ) ;
#103056=ADVANCED_FACE ( 'NONE', ( #27444 ), #15826, .F. ) ;
#103057=EDGE_CURVE ( 'NONE', #82496, #107486, #114464, .T. ) ;
#103059=VECTOR ( 'NONE', #87504, 1000.000000000000000 ) ;
#103060=FACE_OUTER_BOUND ( 'NONE', #104725, .T. ) ;
#103061=EDGE_CURVE ( 'NONE', #91612, #20734, #124640, .T. ) ;
#103062=ORIENTED_EDGE ( 'NONE', *, *, #128918, .T. ) ;
#103063=VECTOR ( 'NONE', #108810, 1000.000000000000000 ) ;
#103064=FACE_OUTER_BOUND ( 'NONE', #111934, .T. ) ;
#103066=ADVANCED_FACE ( 'NONE', ( #91327 ), #125364, .T. ) ;
#103067=LINE ( 'NONE', #115315, #118483 ) ;
#103068=FACE_OUTER_BOUND ( 'NONE', #12910, .T. ) ;
#103069=DIRECTION ( 'NONE',  ( -0.7071067811865486830, -0.7071067811865464625, -0.000000000000000000 ) ) ;
#103073=FACE_OUTER_BOUND ( 'NONE', #81774, .T. ) ;
#103074=ORIENTED_EDGE ( 'NONE', *, *, #100282, .F. ) ;
#103075=ORIENTED_EDGE ( 'NONE', *, *, #71154, .F. ) ;
#103078=EDGE_CURVE ( 'NONE', #113229, #17021, #25314, .T. ) ;
#103079=ORIENTED_EDGE ( 'NONE', *, *, #77063, .T. ) ;
#103080=ORIENTED_EDGE ( 'NONE', *, *, #136838, .F. ) ;
#103082=FACE_OUTER_BOUND ( 'NONE', #83386, .T. ) ;
#103083=CARTESIAN_POINT ( 'NONE',  ( 23.27718569542924243, -21.72500000000000142, 5.000000000000000000 ) ) ;
#103084=ORIENTED_EDGE ( 'NONE', *, *, #62733, .F. ) ;
#103085=DIRECTION ( 'NONE',  ( 0.7071067811865486830, -0.7071067811865464625, -0.000000000000000000 ) ) ;
#103086=EDGE_CURVE ( 'NONE', #110589, #103699, #104289, .T. ) ;
#103087=LINE ( 'NONE', #114650, #143539 ) ;
#103088=PLANE ( 'NONE',  #25579 ) ;
#103090=ORIENTED_EDGE ( 'NONE', *, *, #53776, .F. ) ;
#103091=FACE_OUTER_BOUND ( 'NONE', #127454, .T. ) ;
#103092=CARTESIAN_POINT ( 'NONE',  ( -30.75860074219774631, 21.72500000000000142, 5.000000000000000000 ) ) ;
#103093=DIRECTION ( 'NONE',  ( -0.3543493200069162685, -0.000000000000000000, -0.9351131265310288487 ) ) ;
#103095=CARTESIAN_POINT ( 'NONE',  ( -39.18398860626899705, 28.73617430169814568, 5.000000000000000000 ) ) ;
#103097=DIRECTION ( 'NONE',  ( 0.7071067811865487940, 0.7071067811865463515, -0.000000000000000000 ) ) ;
#103098=DIRECTION ( 'NONE',  ( 0.7071067811865487940, 0.7071067811865463515, 0.000000000000000000 ) ) ;
#103100=LINE ( 'NONE', #5886, #477 ) ;
#103101=ORIENTED_EDGE ( 'NONE', *, *, #133729, .T. ) ;
#103104=ORIENTED_EDGE ( 'NONE', *, *, #54489, .F. ) ;
#103105=VERTEX_POINT ( 'NONE', #69582 ) ;
#103106=CARTESIAN_POINT ( 'NONE',  ( -32.99999999999976552, -10.06887692260770883, 4.000000000000000000 ) ) ;
#103107=CARTESIAN_POINT ( 'NONE',  ( 0.2997448713915885632, -27.71228299555206220, 4.000000000000000000 ) ) ;
#103108=ORIENTED_EDGE ( 'NONE', *, *, #86257, .T. ) ;
#103113=ORIENTED_EDGE ( 'NONE', *, *, #55648, .F. ) ;
#103114=EDGE_CURVE ( 'NONE', #17152, #4875, #26753, .T. ) ;
#103116=VERTEX_POINT ( 'NONE', #35536 ) ;
#103118=DIRECTION ( 'NONE',  ( -0.7071067811865487940, 0.7071067811865463515, -0.000000000000000000 ) ) ;
#103119=EDGE_CURVE ( 'NONE', #106612, #142261, #14456, .T. ) ;
#103120=CARTESIAN_POINT ( 'NONE',  ( 75.18398860626899705, 28.73617430169839793, 5.000000000000000000 ) ) ;
#103121=ORIENTED_EDGE ( 'NONE', *, *, #51544, .T. ) ;
#103122=ORIENTED_EDGE ( 'NONE', *, *, #47003, .T. ) ;
#103123=DIRECTION ( 'NONE',  ( -0.6830127018922181881, 0.6830127018922202975, -0.2588190451025214056 ) ) ;
#103125=LINE ( 'NONE', #137912, #80211 ) ;
#103126=EDGE_CURVE ( 'NONE', #118697, #137485, #101454, .T. ) ;
#103127=VECTOR ( 'NONE', #6777, 1000.000000000000000 ) ;
#103129=VECTOR ( 'NONE', #40385, 1000.000000000000000 ) ;
#103131=EDGE_CURVE ( 'NONE', #125931, #1788, #2102, .T. ) ;
#103132=LINE ( 'NONE', #59655, #117198 ) ;
#103133=VERTEX_POINT ( 'NONE', #79768 ) ;
#103134=EDGE_LOOP ( 'NONE', ( #76520, #76880, #17393, #104660, #63400, #4208 ) ) ;
#103136=VERTEX_POINT ( 'NONE', #13707 ) ;
#103137=AXIS2_PLACEMENT_3D ( 'NONE', #15656, #59945, #38189 ) ;
#103138=DIRECTION ( 'NONE',  ( 0.7071067811865487940, -0.7071067811865463515, 0.000000000000000000 ) ) ;
#103139=ORIENTED_EDGE ( 'NONE', *, *, #34919, .T. ) ;
#103140=PLANE ( 'NONE',  #60829 ) ;
#103142=EDGE_CURVE ( 'NONE', #134353, #132741, #58000, .T. ) ;
#103143=FACE_BOUND ( 'NONE', #125999, .T. ) ;
#103144=PLANE ( 'NONE',  #41036 ) ;
#103146=EDGE_CURVE ( 'NONE', #14576, #34692, #30324, .T. ) ;
#103149=ORIENTED_EDGE ( 'NONE', *, *, #57092, .T. ) ;
#103150=DIRECTION ( 'NONE',  ( 0.6830127018922181881, 0.6830127018922202975, -0.2588190451025214056 ) ) ;
#103151=VECTOR ( 'NONE', #61585, 1000.000000000000000 ) ;
#103152=ORIENTED_EDGE ( 'NONE', *, *, #75422, .T. ) ;
#103153=AXIS2_PLACEMENT_3D ( 'NONE', #27481, #94168, #72482 ) ;
#103154=ORIENTED_EDGE ( 'NONE', *, *, #140456, .T. ) ;
#103156=ORIENTED_EDGE ( 'NONE', *, *, #141765, .F. ) ;
#103157=VECTOR ( 'NONE', #25443, 1000.000000000000000 ) ;
#103158=CYLINDRICAL_SURFACE ( 'NONE', #97321, 0.5000000000000004441 ) ;
#103159=ORIENTED_EDGE ( 'NONE', *, *, #109610, .F. ) ;
#103160=LINE ( 'NONE', #80722, #79203 ) ;
#103161=VECTOR ( 'NONE', #54074, 1000.000000000000000 ) ;
#103162=EDGE_CURVE ( 'NONE', #42123, #118497, #130369, .T. ) ;
#103163=FACE_OUTER_BOUND ( 'NONE', #109202, .T. ) ;
#103164=EDGE_CURVE ( 'NONE', #50292, #23319, #128226, .T. ) ;
#103165=DIRECTION ( 'NONE',  ( -0.3543493200069162685, -0.000000000000000000, -0.9351131265310288487 ) ) ;
#103166=CARTESIAN_POINT ( 'NONE',  ( -12.41161490594822681, 22.22500000000000142, 4.777194822843815025 ) ) ;
#103167=DIRECTION ( 'NONE',  ( -0.3543493200069162685, -0.000000000000000000, -0.9351131265310288487 ) ) ;
#103168=CARTESIAN_POINT ( 'NONE',  ( -48.48921356237309510, -27.52281430457089328, 5.000000000000000000 ) ) ;
#103169=DIRECTION ( 'NONE',  ( -0.7071067811865487940, 0.7071067811865463515, 0.000000000000000000 ) ) ;
#103172=CARTESIAN_POINT ( 'NONE',  ( 34.92499999999998295, 5.831225763041736343, -1.212213889845644488 ) ) ;
#103173=DIRECTION ( 'NONE',  ( 0.7071067811865487940, 0.7071067811865463515, 0.000000000000000000 ) ) ;
#103174=VERTEX_POINT ( 'NONE', #6372 ) ;
#103176=VERTEX_POINT ( 'NONE', #19444 ) ;
#103177=EDGE_CURVE ( 'NONE', #85323, #141546, #115872, .T. ) ;
#103179=EDGE_LOOP ( 'NONE', ( #44420, #138506, #117282, #80666 ) ) ;
#103180=CARTESIAN_POINT ( 'NONE',  ( 25.49999999999982236, -10.04351517176476172, -1.623559851933764175 ) ) ;
#103183=CARTESIAN_POINT ( 'NONE',  ( 34.75611968250419181, -0.1870657452926086095, 4.955485411084880276 ) ) ;
#103184=VERTEX_POINT ( 'NONE', #72450 ) ;
#103185=DIRECTION ( 'NONE',  ( -0.6830127018922180770, -0.6830127018922204085, -0.2588190451025213501 ) ) ;
#103188=CARTESIAN_POINT ( 'NONE',  ( 26.99999999999980815, -9.033600742197647193, 5.000000000000000000 ) ) ;
#103189=EDGE_LOOP ( 'NONE', ( #28583, #138478, #82011, #97047 ) ) ;
#103190=ORIENTED_EDGE ( 'NONE', *, *, #17370, .T. ) ;
#103191=DIRECTION ( 'NONE',  ( 0.7071067811865487940, 0.7071067811865463515, 0.000000000000000000 ) ) ;
#103192=LINE ( 'NONE', #48840, #19079 ) ;
#103194=ORIENTED_EDGE ( 'NONE', *, *, #100458, .F. ) ;
#103195=LINE ( 'NONE', #81488, #124660 ) ;
#103196=DIRECTION ( 'NONE',  ( 0.6830127018922181881, 0.6830127018922202975, -0.2588190451025214056 ) ) ;
#103197=CARTESIAN_POINT ( 'NONE',  ( -34.49999999999975842, 10.94296225409023116, -9.576120664313334530 ) ) ;
#103198=CARTESIAN_POINT ( 'NONE',  ( 34.49999999999976552, 3.054329344830917670, 4.994342998332163219 ) ) ;
#103199=PLANE ( 'NONE',  #99985 ) ;
#103200=VERTEX_POINT ( 'NONE', #86140 ) ;
#103202=PLANE ( 'NONE',  #102550 ) ;
#103204=DIRECTION ( 'NONE',  ( 1.000000000000000000, 0.000000000000000000, 0.000000000000000000 ) ) ;
#103206=VERTEX_POINT ( 'NONE', #118003 ) ;
#103207=ORIENTED_EDGE ( 'NONE', *, *, #103230, .T. ) ;
#103208=CARTESIAN_POINT ( 'NONE',  ( -31.17183060077625711, 0.7592924766157069794, 4.000000000000000000 ) ) ;
#103209=CARTESIAN_POINT ( 'NONE',  ( 16.49999999999989342, -7.912538124160671593, 4.000000000000000000 ) ) ;
#103211=VECTOR ( 'NONE', #39596, 1000.000000000000000 ) ;
#103212=CARTESIAN_POINT ( 'NONE',  ( 11.20710678118646619, -14.24070752338413648, 5.000000000000000000 ) ) ;
#103213=ADVANCED_FACE ( 'NONE', ( #94838 ), #17300, .F. ) ;
#103214=LINE ( 'NONE', #81507, #20636 ) ;
#103215=LINE ( 'NONE', #58357, #69221 ) ;
#103216=PLANE ( 'NONE',  #44471 ) ;
#103217=EDGE_CURVE ( 'NONE', #36268, #116539, #141212, .T. ) ;
#103218=ADVANCED_FACE ( 'NONE', ( #62984 ), #16571, .F. ) ;
#103221=CARTESIAN_POINT ( 'NONE',  ( -26.99999999999981171, 20.70535890316558891, 1.956823837851977332 ) ) ;
#103222=EDGE_CURVE ( 'NONE', #72201, #24821, #95573, .T. ) ;
#103226=DIRECTION ( 'NONE',  ( 0.7071067811865487940, 0.7071067811865463515, 0.000000000000000000 ) ) ;
#103227=FACE_OUTER_BOUND ( 'NONE', #17131, .T. ) ;
#103228=VERTEX_POINT ( 'NONE', #105712 ) ;
#103229=AXIS2_PLACEMENT_3D ( 'NONE', #120705, #63529, #42484 ) ;
#103230=EDGE_CURVE ( 'NONE', #99775, #45656, #18705, .T. ) ;
#103231=LINE ( 'NONE', #95749, #21076 ) ;
#103232=ORIENTED_EDGE ( 'NONE', *, *, #129255, .T. ) ;
#103233=CARTESIAN_POINT ( 'NONE',  ( 14.18753812416042948, -22.22500000000000142, 4.000000000000000000 ) ) ;
#103234=CARTESIAN_POINT ( 'NONE',  ( 33.32816939922329880, 11.25929247661559529, 4.000000000000000000 ) ) ;
#103235=DIRECTION ( 'NONE',  ( 0.3543493200069162685, -0.000000000000000000, -0.9351131265310288487 ) ) ;
#103237=DIRECTION ( 'NONE',  ( 0.7071067811865486830, -0.7071067811865464625, -0.000000000000000000 ) ) ;
#103239=DIRECTION ( 'NONE',  ( 0.6830127018922181881, 0.6830127018922202975, -0.2588190451025214056 ) ) ;
#103240=CARTESIAN_POINT ( 'NONE',  ( 8.999999999999937828, -4.068876922607770119, 4.000000000000000000 ) ) ;
#103241=EDGE_LOOP ( 'NONE', ( #19306, #104941, #34205, #119136 ) ) ;
#103242=DIRECTION ( 'NONE',  ( -0.6830127018922180770, -0.6830127018922204085, -0.2588190451025213501 ) ) ;
#103243=FACE_OUTER_BOUND ( 'NONE', #1113, .T. ) ;
#103244=CARTESIAN_POINT ( 'NONE',  ( 29.67183060077625711, 2.259292476615694323, 4.000000000000000000 ) ) ;
#103247=CARTESIAN_POINT ( 'NONE',  ( -34.42500000000001137, 11.97718569542929856, 5.000000000000000000 ) ) ;
#103249=VECTOR ( 'NONE', #10372, 1000.000000000000000 ) ;
#103251=ORIENTED_EDGE ( 'NONE', *, *, #136704, .T. ) ;
#103252=ORIENTED_EDGE ( 'NONE', *, *, #130845, .T. ) ;
#103254=DIRECTION ( 'NONE',  ( 0.7071067811865487940, -0.7071067811865463515, 0.000000000000000000 ) ) ;
#103255=DIRECTION ( 'NONE',  ( 0.7071067811865487940, 0.7071067811865463515, -0.000000000000000000 ) ) ;
#103258=ORIENTED_EDGE ( 'NONE', *, *, #101343, .F. ) ;
#103259=CARTESIAN_POINT ( 'NONE',  ( -24.18398860626899705, 28.73617430169804265, 5.000000000000000000 ) ) ;
#103262=EDGE_CURVE ( 'NONE', #99727, #125649, #67244, .T. ) ;
#103263=LINE ( 'NONE', #48187, #110767 ) ;
#103264=ORIENTED_EDGE ( 'NONE', *, *, #40569, .F. ) ;
#103265=ORIENTED_EDGE ( 'NONE', *, *, #18485, .T. ) ;
#103266=CARTESIAN_POINT ( 'NONE',  ( 25.82816939922335209, -17.24070752338409918, 4.000000000000000000 ) ) ;
#103267=LINE ( 'NONE', #102590, #59216 ) ;
#103268=DIRECTION ( 'NONE',  ( 0.7071067811865487940, 0.7071067811865463515, 0.000000000000000000 ) ) ;
#103269=CARTESIAN_POINT ( 'NONE',  ( 17.99451991528748351, 28.92564299267950645, 4.000000000000000000 ) ) ;
#103270=LINE ( 'NONE', #35921, #76373 ) ;
#103271=DIRECTION ( 'NONE',  ( -0.000000000000000000, -0.3543493200069152693, 0.9351131265310292928 ) ) ;
#103272=ORIENTED_EDGE ( 'NONE', *, *, #47177, .T. ) ;
#103273=CARTESIAN_POINT ( 'NONE',  ( 21.18398860626899349, 28.73617430169802134, 5.000000000000000000 ) ) ;
#103274=DIRECTION ( 'NONE',  ( -0.7071067811865486830, 0.7071067811865464625, 0.000000000000000000 ) ) ;
#103277=VERTEX_POINT ( 'NONE', #121600 ) ;
#103278=EDGE_LOOP ( 'NONE', ( #84636, #121496, #58118, #989 ) ) ;
#103279=CARTESIAN_POINT ( 'NONE',  ( 11.81601139373100651, 28.73617430169779041, 5.000000000000000000 ) ) ;
#103280=CARTESIAN_POINT ( 'NONE',  ( -7.628234450443801329, -8.240707523384200428, 11.38925528200754300 ) ) ;
#103282=FACE_OUTER_BOUND ( 'NONE', #119648, .T. ) ;
#103283=DIRECTION ( 'NONE',  ( -0.6830127018922180770, -0.6830127018922204085, -0.2588190451025213501 ) ) ;
#103284=ORIENTED_EDGE ( 'NONE', *, *, #107470, .T. ) ;
#103285=ORIENTED_EDGE ( 'NONE', *, *, #88142, .T. ) ;
#103287=CARTESIAN_POINT ( 'NONE',  ( 4.499999999999972466, -10.53360074219763298, 5.000000000000000000 ) ) ;
#103288=CARTESIAN_POINT ( 'NONE',  ( 50.99451991528749062, 28.92564299267973738, 4.000000000000000000 ) ) ;
#103289=ORIENTED_EDGE ( 'NONE', *, *, #30964, .F. ) ;
#103290=EDGE_CURVE ( 'NONE', #84395, #84525, #75279, .T. ) ;
#103292=ORIENTED_EDGE ( 'NONE', *, *, #1541, .T. ) ;
#103294=DIRECTION ( 'NONE',  ( 1.000000000000000000, 0.000000000000000000, 0.000000000000000000 ) ) ;
#103295=AXIS2_PLACEMENT_3D ( 'NONE', #104665, #60488, #6029 ) ;
#103296=ORIENTED_EDGE ( 'NONE', *, *, #62124, .T. ) ;
#103297=EDGE_CURVE ( 'NONE', #28284, #78029, #65122, .T. ) ;
#103298=FACE_BOUND ( 'NONE', #84886, .T. ) ;
#103299=CARTESIAN_POINT ( 'NONE',  ( -27.48921356237309155, -27.52281430457074762, 5.000000000000000000 ) ) ;
#103300=FACE_OUTER_BOUND ( 'NONE', #137260, .T. ) ;
#103301=DIRECTION ( 'NONE',  ( 0.7071067811865487940, 0.7071067811865463515, 0.000000000000000000 ) ) ;
#103304=VERTEX_POINT ( 'NONE', #120888 ) ;
#103305=ORIENTED_EDGE ( 'NONE', *, *, #46163, .F. ) ;
#103307=ORIENTED_EDGE ( 'NONE', *, *, #69726, .T. ) ;
#103309=CARTESIAN_POINT ( 'NONE',  ( 5.671830600776425868, -18.74070752338409207, 4.000000000000000000 ) ) ;
#103310=CARTESIAN_POINT ( 'NONE',  ( -21.18398860626899349, 28.73617430169802134, 5.000000000000000000 ) ) ;
#103311=SHAPE_REPRESENTATION ( '1.3 Jaw Plate', ( #127880 ), #137188 ) ;
#103312=DIRECTION ( 'NONE',  ( 0.7071067811865487940, 0.7071067811865463515, 0.000000000000000000 ) ) ;
#103313=EDGE_LOOP ( 'NONE', ( #45726, #1471, #134648, #143202 ) ) ;
#103314=CARTESIAN_POINT ( 'NONE',  ( 33.32816939922331301, -21.74070752338405654, 4.000000000000000000 ) ) ;
#103315=EDGE_CURVE ( 'NONE', #118046, #25524, #43352, .T. ) ;
#103317=CARTESIAN_POINT ( 'NONE',  ( -23.99451991528749062, 28.92564299267954908, 4.000000000000000000 ) ) ;
#103318=DIRECTION ( 'NONE',  ( -0.000000000000000000, -0.3543493200069152693, 0.9351131265310292928 ) ) ;
#103319=FACE_OUTER_BOUND ( 'NONE', #119042, .T. ) ;
#103320=CARTESIAN_POINT ( 'NONE',  ( 17.67183060077635304, 17.25929247661554200, 4.000000000000000000 ) ) ;
#103321=VERTEX_POINT ( 'NONE', #9994 ) ;
#103322=LINE ( 'NONE', #93186, #121327 ) ;
#103323=LINE ( 'NONE', #3973, #37308 ) ;
#103324=ORIENTED_EDGE ( 'NONE', *, *, #143075, .F. ) ;
#103325=EDGE_CURVE ( 'NONE', #36965, #87041, #33226, .T. ) ;
#103326=VECTOR ( 'NONE', #106457, 999.9999999999998863 ) ;
#103327=VERTEX_POINT ( 'NONE', #86861 ) ;
#103328=ADVANCED_FACE ( 'NONE', ( #12126 ), #78130, .T. ) ;
#103329=ORIENTED_EDGE ( 'NONE', *, *, #128969, .T. ) ;
#103331=EDGE_LOOP ( 'NONE', ( #78567, #12968, #60294, #5027 ) ) ;
#103332=VECTOR ( 'NONE', #103973, 1000.000000000000000 ) ;
#103334=AXIS2_PLACEMENT_3D ( 'NONE', #1894, #35326, #12097 ) ;
#103337=ORIENTED_EDGE ( 'NONE', *, *, #25353, .T. ) ;
#103338=LINE ( 'NONE', #24375, #126654 ) ;
#103340=FACE_OUTER_BOUND ( 'NONE', #116436, .T. ) ;
#103341=CIRCLE ( 'NONE', #89501, 5.968999999999998529 ) ;
#103344=VERTEX_POINT ( 'NONE', #108553 ) ;
#103345=ORIENTED_EDGE ( 'NONE', *, *, #77404, .T. ) ;
#103347=CARTESIAN_POINT ( 'NONE',  ( 0.000000000000000000, 0.000000000000000000, 5.000000000000000000 ) ) ;
#103348=CARTESIAN_POINT ( 'NONE',  ( -6.299744871391586898, -27.71228299555210484, 4.000000000000000000 ) ) ;
#103350=VERTEX_POINT ( 'NONE', #133234 ) ;
#103353=VERTEX_POINT ( 'NONE', #65858 ) ;
#103355=ORIENTED_EDGE ( 'NONE', *, *, #122441, .F. ) ;
#103357=DIRECTION ( 'NONE',  ( 0.7071067811865487940, -0.7071067811865463515, 0.000000000000000000 ) ) ;
#103358=LINE ( 'NONE', #4008, #60190 ) ;
#103359=DIRECTION ( 'NONE',  ( -0.000000000000000000, -0.3543493200069152693, 0.9351131265310292928 ) ) ;
#103363=DIRECTION ( 'NONE',  ( 0.6830127018922180770, -0.6830127018922204085, -0.2588190451025213501 ) ) ;
#103364=ADVANCED_FACE ( 'NONE', ( #110013 ), #89699, .F. ) ;
#103365=VECTOR ( 'NONE', #85348, 999.9999999999998863 ) ;
#103366=CARTESIAN_POINT ( 'NONE',  ( 0.000000000000000000, 0.000000000000000000, 5.000000000000000000 ) ) ;
#103368=EDGE_LOOP ( 'NONE', ( #138274, #56595, #35287, #76216 ) ) ;
#103369=EDGE_CURVE ( 'NONE', #66646, #17336, #44068, .T. ) ;
#103370=VERTEX_POINT ( 'NONE', #132536 ) ;
#103371=EDGE_LOOP ( 'NONE', ( #85942, #83752, #19385, #49203 ) ) ;
#103372=FACE_OUTER_BOUND ( 'NONE', #108033, .T. ) ;
#103373=CARTESIAN_POINT ( 'NONE',  ( 4.499999999999974243, 1.466399257802244893, 5.000000000000000000 ) ) ;
#103376=DIRECTION ( 'NONE',  ( 0.7071067811865486830, -0.7071067811865464625, -0.000000000000000000 ) ) ;
#103377=DIRECTION ( 'NONE',  ( -0.7071067811865487940, 0.7071067811865463515, 0.000000000000000000 ) ) ;
#103378=EDGE_CURVE ( 'NONE', #26153, #48148, #33911, .T. ) ;
#103380=EDGE_CURVE ( 'NONE', #93894, #56990, #1237, .T. ) ;
#103381=CARTESIAN_POINT ( 'NONE',  ( -41.99451991528749062, 28.92564299267967343, 4.000000000000000000 ) ) ;
#103382=CARTESIAN_POINT ( 'NONE',  ( -5.999999999999954703, -21.03360074219752462, 5.000000000000000000 ) ) ;
#103383=DIRECTION ( 'NONE',  ( -0.3543493200069162685, -0.000000000000000000, -0.9351131265310288487 ) ) ;
#103384=CARTESIAN_POINT ( 'NONE',  ( -22.49999999999984723, -1.592773361805393417, -6.492772025301177585 ) ) ;
#103387=ORIENTED_EDGE ( 'NONE', *, *, #105834, .F. ) ;
#103390=DIRECTION ( 'NONE',  ( -0.6830127018922180770, -0.6830127018922204085, -0.2588190451025213501 ) ) ;
#103391=CARTESIAN_POINT ( 'NONE',  ( 30.48921356237309510, -27.52281430457076894, 5.000000000000000000 ) ) ;
#103392=ORIENTED_EDGE ( 'NONE', *, *, #53108, .F. ) ;
#103393=EDGE_CURVE ( 'NONE', #99617, #55336, #89014, .T. ) ;
#103395=EDGE_CURVE ( 'NONE', #63781, #31625, #18654, .T. ) ;
#103396=CARTESIAN_POINT ( 'NONE',  ( -80.99451991528748351, 28.92564299267994699, 4.000000000000000000 ) ) ;
#103397=DIRECTION ( 'NONE',  ( 0.7071067811865487940, 0.7071067811865463515, 0.000000000000000000 ) ) ;
#103398=EDGE_LOOP ( 'NONE', ( #58515, #61465, #128961, #47063 ) ) ;
#103399=DIRECTION ( 'NONE',  ( -0.000000000000000000, 0.3543493200069153248, 0.9351131265310292928 ) ) ;
#103400=VERTEX_POINT ( 'NONE', #112188 ) ;
#103402=ORIENTED_EDGE ( 'NONE', *, *, #20892, .T. ) ;
#103403=CARTESIAN_POINT ( 'NONE',  ( -13.49999999999990408, -16.91253812416058722, 4.000000000000000000 ) ) ;
#103404=EDGE_CURVE ( 'NONE', #103813, #52412, #69397, .T. ) ;
#103407=DIRECTION ( 'NONE',  ( -0.6830127018922181881, 0.6830127018922202975, -0.2588190451025214056 ) ) ;
#103408=DIRECTION ( 'NONE',  ( 0.7071067811865487940, -0.7071067811865463515, 0.000000000000000000 ) ) ;
#103409=ORIENTED_EDGE ( 'NONE', *, *, #114762, .F. ) ;
#103412=LINE ( 'NONE', #123786, #132968 ) ;
#103413=LINE ( 'NONE', #57111, #127173 ) ;
#103416=ADVANCED_FACE ( 'NONE', ( #114306 ), #13540, .F. ) ;
#103417=CARTESIAN_POINT ( 'NONE',  ( -31.49999999999977973, -11.56887692260769640, 4.000000000000000000 ) ) ;
#103418=VERTEX_POINT ( 'NONE', #78849 ) ;
#103420=EDGE_LOOP ( 'NONE', ( #64909, #70817, #11264, #97951 ) ) ;
#103422=CARTESIAN_POINT ( 'NONE',  ( 7.358242975411349640, 15.75929247661555088, 19.34181609438697791 ) ) ;
#103423=FACE_OUTER_BOUND ( 'NONE', #52183, .T. ) ;
#103424=ADVANCED_FACE ( 'NONE', ( #3380 ), #36060, .F. ) ;
#103425=CARTESIAN_POINT ( 'NONE',  ( 34.47516574401890921, 19.49051761211542910, 4.998110765256835286 ) ) ;
#103428=LINE ( 'NONE', #48358, #35018 ) ;
#103429=DIRECTION ( 'NONE',  ( 0.7071067811865487940, -0.7071067811865463515, 0.000000000000000000 ) ) ;
#103430=VECTOR ( 'NONE', #70007, 1000.000000000000000 ) ;
#103431=ORIENTED_EDGE ( 'NONE', *, *, #140576, .T. ) ;
#103432=FACE_OUTER_BOUND ( 'NONE', #51473, .T. ) ;
#103433=LINE ( 'NONE', #49822, #70319 ) ;
#103435=EDGE_LOOP ( 'NONE', ( #8389, #79014, #47026, #53198 ) ) ;
#103436=EDGE_CURVE ( 'NONE', #22222, #65695, #90414, .T. ) ;
#103437=DIRECTION ( 'NONE',  ( 0.7071067811865487940, -0.7071067811865463515, 0.000000000000000000 ) ) ;
#103438=DIRECTION ( 'NONE',  ( -0.000000000000000000, 0.3543493200069153248, 0.9351131265310292928 ) ) ;
#103439=DIRECTION ( 'NONE',  ( -0.000000000000000000, 0.000000000000000000, 1.000000000000000000 ) ) ;
#103443=ORIENTED_EDGE ( 'NONE', *, *, #104357, .F. ) ;
#103444=ADVANCED_FACE ( 'NONE', ( #70834 ), #135381, .F. ) ;
#103445=ORIENTED_EDGE ( 'NONE', *, *, #28891, .F. ) ;
#103446=ORIENTED_EDGE ( 'NONE', *, *, #119971, .T. ) ;
#103447=VECTOR ( 'NONE', #73158, 1000.000000000000000 ) ;
#103449=ORIENTED_EDGE ( 'NONE', *, *, #110691, .F. ) ;
#103451=AXIS2_PLACEMENT_3D ( 'NONE', #8548, #54287, #110039 ) ;
#103452=DIRECTION ( 'NONE',  ( -0.7071067811865486830, -0.7071067811865464625, -0.000000000000000000 ) ) ;
#103453=LINE ( 'NONE', #82448, #135960 ) ;
#103456=VERTEX_POINT ( 'NONE', #23732 ) ;
#103458=LINE ( 'NONE', #47020, #134724 ) ;
#103461=CARTESIAN_POINT ( 'NONE',  ( 11.99999999999992184, 10.55218569542905982, 5.000000000000000000 ) ) ;
#103462=LINE ( 'NONE', #117186, #73376 ) ;
#103463=DIRECTION ( 'NONE',  ( -0.7071067811865486830, 0.7071067811865464625, 0.000000000000000000 ) ) ;
#103465=ORIENTED_EDGE ( 'NONE', *, *, #47312, .T. ) ;
#103470=AXIS2_PLACEMENT_3D ( 'NONE', #77012, #142944, #81 ) ;
#103471=DIRECTION ( 'NONE',  ( 0.7071067811865487940, 0.7071067811865463515, 0.000000000000000000 ) ) ;
#103472=DIRECTION ( 'NONE',  ( -0.7071067811865486830, 0.7071067811865464625, 0.000000000000000000 ) ) ;
#103473=VECTOR ( 'NONE', #959, 1000.000000000000000 ) ;
#103474=ORIENTED_EDGE ( 'NONE', *, *, #113531, .F. ) ;
#103476=ORIENTED_EDGE ( 'NONE', *, *, #43913, .F. ) ;
#103477=CARTESIAN_POINT ( 'NONE',  ( 20.67183060077632462, -15.74070752338412760, 4.000000000000000000 ) ) ;
#103478=ORIENTED_EDGE ( 'NONE', *, *, #127783, .F. ) ;
#103479=EDGE_CURVE ( 'NONE', #113815, #20046, #103412, .T. ) ;
#103480=VECTOR ( 'NONE', #134704, 1000.000000000000227 ) ;
#103481=LINE ( 'NONE', #56490, #61311 ) ;
#103482=ORIENTED_EDGE ( 'NONE', *, *, #101302, .F. ) ;
#103485=VECTOR ( 'NONE', #124655, 1000.000000000000000 ) ;
#103486=CARTESIAN_POINT ( 'NONE',  ( 0.2997448713915885632, -27.71228299555206220, 4.000000000000000000 ) ) ;
#103487=FACE_OUTER_BOUND ( 'NONE', #85657, .T. ) ;
#103488=ORIENTED_EDGE ( 'NONE', *, *, #135022, .F. ) ;
#103489=DIRECTION ( 'NONE',  ( 1.000000000000000000, 0.000000000000000000, 0.000000000000000000 ) ) ;
#103490=FACE_OUTER_BOUND ( 'NONE', #64161, .T. ) ;
#103491=VECTOR ( 'NONE', #17888, 1000.000000000000000 ) ;
#103492=ORIENTED_EDGE ( 'NONE', *, *, #32301, .F. ) ;
#103494=CARTESIAN_POINT ( 'NONE',  ( 2.999999999999976463, 10.55218569542906160, 5.000000000000000000 ) ) ;
#103495=ORIENTED_EDGE ( 'NONE', *, *, #77486, .T. ) ;
#103496=EDGE_LOOP ( 'NONE', ( #47221, #129411, #95528, #119519 ) ) ;
#103497=LINE ( 'NONE', #126681, #78327 ) ;
#103498=EDGE_CURVE ( 'NONE', #41303, #119060, #79601, .T. ) ;
#103499=EDGE_LOOP ( 'NONE', ( #139634, #100830, #126229, #53977 ) ) ;
#103500=ORIENTED_EDGE ( 'NONE', *, *, #66831, .F. ) ;
#103503=CARTESIAN_POINT ( 'NONE',  ( -20.99999999999985789, -16.60178936734450872, 0.8616154019347020965 ) ) ;
#103504=CARTESIAN_POINT ( 'NONE',  ( 21.47336096364202263, -5.240707523384221744, 16.25846745537500482 ) ) ;
#103505=VECTOR ( 'NONE', #27008, 1000.000000000000000 ) ;
#103507=DIRECTION ( 'NONE',  ( 0.3543493200069162685, -0.000000000000000000, -0.9351131265310288487 ) ) ;
#103508=ADVANCED_FACE ( 'NONE', ( #14279 ), #58564, .F. ) ;
#103509=CARTESIAN_POINT ( 'NONE',  ( 18.48921356237309510, -27.52281430457068367, 5.000000000000000000 ) ) ;
#103510=CARTESIAN_POINT ( 'NONE',  ( -34.92500000000001137, 21.72500000000000142, 4.165035510187084178 ) ) ;
#103513=EDGE_CURVE ( 'NONE', #139146, #37315, #91834, .T. ) ;
#103514=LINE ( 'NONE', #62192, #49124 ) ;
#103515=VERTEX_POINT ( 'NONE', #51026 ) ;
#103516=LINE ( 'NONE', #48448, #10998 ) ;
#103517=PLANE ( 'NONE',  #33757 ) ;
#103518=EDGE_LOOP ( 'NONE', ( #32177, #98363, #85266, #71829 ) ) ;
#103519=ORIENTED_EDGE ( 'NONE', *, *, #22386, .F. ) ;
#103521=EDGE_CURVE ( 'NONE', #69963, #68778, #25873, .T. ) ;
#103522=VERTEX_POINT ( 'NONE', #37483 ) ;
#103523=CARTESIAN_POINT ( 'NONE',  ( 13.49999999999991473, -8.947814304570734123, 5.000000000000000000 ) ) ;
#103524=DIRECTION ( 'NONE',  ( -0.6830127018922181881, 0.6830127018922202975, -0.2588190451025214056 ) ) ;
#103525=VECTOR ( 'NONE', #88356, 999.9999999999998863 ) ;
#103526=DIRECTION ( 'NONE',  ( 1.000000000000000000, 0.000000000000000000, 0.000000000000000000 ) ) ;
#103527=DIRECTION ( 'NONE',  ( -0.000000000000000000, 0.000000000000000000, 1.000000000000000000 ) ) ;
#103528=ORIENTED_EDGE ( 'NONE', *, *, #114506, .F. ) ;
#103529=LINE ( 'NONE', #60813, #58117 ) ;
#103530=ORIENTED_EDGE ( 'NONE', *, *, #37728, .F. ) ;
#103532=VECTOR ( 'NONE', #81786, 1000.000000000000000 ) ;
#103533=DIRECTION ( 'NONE',  ( 0.6830127018922181881, 0.6830127018922202975, -0.2588190451025214056 ) ) ;
#103534=( BOUNDED_CURVE ( )  B_SPLINE_CURVE ( 3, ( #17691, #4629, #138074, #38761 ),
 .UNSPECIFIED., .F., .T. ) 
 B_SPLINE_CURVE_WITH_KNOTS ( ( 4, 4 ),
 ( 5.106027341939283204, 6.645403452391245303 ),
 .UNSPECIFIED. ) 
 CURVE ( )  GEOMETRIC_REPRESENTATION_ITEM ( )  RATIONAL_B_SPLINE_CURVE ( ( 1.000000000000000000, 0.8120851936182283959, 0.8120851936182283959, 1.000000000000000000 ) ) 
 REPRESENTATION_ITEM ( '' )  );
#103536=CARTESIAN_POINT ( 'NONE',  ( 8.510786437626906675, -27.52281430457049183, 5.000000000000000000 ) ) ;
#103537=CARTESIAN_POINT ( 'NONE',  ( 26.99451991528749417, 28.92564299267956685, 4.000000000000000000 ) ) ;
#103539=EDGE_CURVE ( 'NONE', #28845, #103024, #4058, .T. ) ;
#103540=ORIENTED_EDGE ( 'NONE', *, *, #16279, .T. ) ;
#103541=ORIENTED_EDGE ( 'NONE', *, *, #116679, .F. ) ;
#103543=CARTESIAN_POINT ( 'NONE',  ( 11.18753812416045434, -22.22500000000000142, 4.000000000000000000 ) ) ;
#103544=VECTOR ( 'NONE', #138610, 1000.000000000000000 ) ;
#103545=LINE ( 'NONE', #115120, #109890 ) ;
#103547=ORIENTED_EDGE ( 'NONE', *, *, #94149, .T. ) ;
#103549=EDGE_CURVE ( 'NONE', #37816, #53397, #26592, .T. ) ;
#103550=EDGE_CURVE ( 'NONE', #135328, #138961, #133925, .T. ) ;
#103552=CARTESIAN_POINT ( 'NONE',  ( 42.48921356237308800, -27.52281430457085065, 5.000000000000000000 ) ) ;
#103553=CARTESIAN_POINT ( 'NONE',  ( -12.31657961132782297, -6.740707523384216415, 11.88629033278126990 ) ) ;
#103554=LINE ( 'NONE', #4191, #88231 ) ;
#103555=CARTESIAN_POINT ( 'NONE',  ( -31.36246187583881806, 22.22499999999999432, 4.000000000000000000 ) ) ;
#103556=EDGE_LOOP ( 'NONE', ( #8867, #27753, #78857, #129903 ) ) ;
#103557=CARTESIAN_POINT ( 'NONE',  ( 66.18398860626901126, 28.73617430169833753, 5.000000000000000000 ) ) ;
#103558=DIRECTION ( 'NONE',  ( 0.7071067811865487940, 0.7071067811865463515, 0.000000000000000000 ) ) ;
#103559=EDGE_CURVE ( 'NONE', #11154, #106829, #32120, .T. ) ;
#103561=LINE ( 'NONE', #57983, #13896 ) ;
#103563=ADVANCED_FACE ( 'NONE', ( #119809 ), #19801, .F. ) ;
#103564=ORIENTED_EDGE ( 'NONE', *, *, #40447, .F. ) ;
#103565=EDGE_CURVE ( 'NONE', #61782, #67530, #64042, .T. ) ;
#103566=LINE ( 'NONE', #76320, #107032 ) ;
#103568=CARTESIAN_POINT ( 'NONE',  ( -57.48921356237308800, -27.52281430457095368, 5.000000000000000000 ) ) ;
#103569=VECTOR ( 'NONE', #2576, 999.9999999999998863 ) ;
#103570=ORIENTED_EDGE ( 'NONE', *, *, #110163, .F. ) ;
#103571=DIRECTION ( 'NONE',  ( 0.6830127018922180770, 0.6830127018922202975, -0.2588190451025213501 ) ) ;
#103572=ORIENTED_EDGE ( 'NONE', *, *, #1376, .F. ) ;
#103573=CARTESIAN_POINT ( 'NONE',  ( 4.499999999999966249, -19.91253812416055169, 4.000000000000000000 ) ) ;
#103576=EDGE_CURVE ( 'NONE', #126581, #57666, #84389, .T. ) ;
#103578=LINE ( 'NONE', #15822, #94827 ) ;
#103579=ADVANCED_FACE ( 'NONE', ( #40179 ), #97341, .T. ) ;
#103580=CARTESIAN_POINT ( 'NONE',  ( 13.26601651615776767, 1.700382741644379081, 5.000000000000000000 ) ) ;
#103581=CARTESIAN_POINT ( 'NONE',  ( 20.20710678118641113, -14.24070752338413826, 5.000000000000000000 ) ) ;
#103582=FACE_OUTER_BOUND ( 'NONE', #63005, .T. ) ;
#103586=VECTOR ( 'NONE', #109894, 1000.000000000000000 ) ;
#103587=ADVANCED_FACE ( 'NONE', ( #128579 ), #109676, .F. ) ;
#103588=DIRECTION ( 'NONE',  ( -0.000000000000000000, 0.3543493200069153248, 0.9351131265310292928 ) ) ;
#103589=CARTESIAN_POINT ( 'NONE',  ( 0.000000000000000000, 0.000000000000000000, 5.000000000000000000 ) ) ;
#103590=ORIENTED_EDGE ( 'NONE', *, *, #33044, .F. ) ;
#103591=ORIENTED_EDGE ( 'NONE', *, *, #89907, .F. ) ;
#103593=ORIENTED_EDGE ( 'NONE', *, *, #105038, .F. ) ;
#103594=EDGE_LOOP ( 'NONE', ( #130459, #1133, #143208, #95974 ) ) ;
#103595=LINE ( 'NONE', #84045, #71935 ) ;
#103596=DIRECTION ( 'NONE',  ( -0.7071067811865486830, -0.7071067811865464625, 0.000000000000000000 ) ) ;
#103598=LINE ( 'NONE', #28920, #113490 ) ;
#103599=LINE ( 'NONE', #113789, #99647 ) ;
#103602=DIRECTION ( 'NONE',  ( -0.6830127018922181881, 0.6830127018922202975, -0.2588190451025214056 ) ) ;
#103603=PLANE ( 'NONE',  #109857 ) ;
#103604=DIRECTION ( 'NONE',  ( 0.7071067811865487940, -0.7071067811865463515, 0.000000000000000000 ) ) ;
#103605=LINE ( 'NONE', #115898, #105417 ) ;
#103606=DIRECTION ( 'NONE',  ( 0.3543493200069162685, -0.000000000000000000, -0.9351131265310288487 ) ) ;
#103608=DIRECTION ( 'NONE',  ( -0.7071067811865487940, 0.7071067811865463515, 0.000000000000000000 ) ) ;
#103609=CARTESIAN_POINT ( 'NONE',  ( 15.48921356237309510, -27.52281430457066236, 5.000000000000000000 ) ) ;
#103610=EDGE_CURVE ( 'NONE', #128178, #25861, #120514, .T. ) ;
#103611=EDGE_CURVE ( 'NONE', #23390, #40720, #74940, .T. ) ;
#103613=VERTEX_POINT ( 'NONE', #142330 ) ;
#103615=AXIS2_PLACEMENT_3D ( 'NONE', #78746, #112785, #23639 ) ;
#103617=CARTESIAN_POINT ( 'NONE',  ( -12.18398860626900060, 28.73617430169795739, 5.000000000000000000 ) ) ;
#103618=DIRECTION ( 'NONE',  ( -0.7071067811865486830, -0.7071067811865464625, 0.000000000000000000 ) ) ;
#103619=VERTEX_POINT ( 'NONE', #19097 ) ;
#103620=EDGE_CURVE ( 'NONE', #8752, #103200, #73497, .T. ) ;
#103621=CARTESIAN_POINT ( 'NONE',  ( -12.48921356237309155, -27.52281430457064104, 5.000000000000000000 ) ) ;
#103622=LINE ( 'NONE', #56633, #111386 ) ;
#103625=ORIENTED_EDGE ( 'NONE', *, *, #87183, .T. ) ;
#103626=ORIENTED_EDGE ( 'NONE', *, *, #129595, .T. ) ;
#103628=DIRECTION ( 'NONE',  ( -0.6830127018922181881, 0.6830127018922202975, -0.2588190451025214056 ) ) ;
#103630=ORIENTED_EDGE ( 'NONE', *, *, #140594, .F. ) ;
#103632=AXIS2_PLACEMENT_3D ( 'NONE', #125805, #1813, #59150 ) ;
#103633=ORIENTED_EDGE ( 'NONE', *, *, #15910, .F. ) ;
#103634=CARTESIAN_POINT ( 'NONE',  ( -24.64327148205084583, 5.259292476615665457, 4.831541298974430632 ) ) ;
#103636=VECTOR ( 'NONE', #20310, 1000.000000000000000 ) ;
#103638=ORIENTED_EDGE ( 'NONE', *, *, #86915, .F. ) ;
#103639=ORIENTED_EDGE ( 'NONE', *, *, #17682, .F. ) ;
#103640=DIRECTION ( 'NONE',  ( -0.7071067811865487940, 0.7071067811865463515, -0.000000000000000000 ) ) ;
#103641=ORIENTED_EDGE ( 'NONE', *, *, #23155, .F. ) ;
#103642=EDGE_LOOP ( 'NONE', ( #19959, #127629, #33567 ) ) ;
#103643=CARTESIAN_POINT ( 'NONE',  ( 4.408325480989981671, -0.7407075233842770334, 14.76736230305381703 ) ) ;
#103644=CARTESIAN_POINT ( 'NONE',  ( 26.67183060077628198, -0.7407075233842665973, 4.000000000000000000 ) ) ;
#103645=ORIENTED_EDGE ( 'NONE', *, *, #76104, .F. ) ;
#103646=CARTESIAN_POINT ( 'NONE',  ( 69.48921356237309510, -27.52281430457103895, 5.000000000000000000 ) ) ;
#103647=DIRECTION ( 'NONE',  ( 0.7071067811865487940, 0.7071067811865463515, 0.000000000000000000 ) ) ;
#103650=CARTESIAN_POINT ( 'NONE',  ( -8.999999999999941380, 1.931123077392167264, 4.000000000000000000 ) ) ;
#103651=FACE_BOUND ( 'NONE', #141283, .T. ) ;
#103652=ORIENTED_EDGE ( 'NONE', *, *, #31891, .T. ) ;
#103654=EDGE_CURVE ( 'NONE', #123427, #41026, #140177, .T. ) ;
#103655=DIRECTION ( 'NONE',  ( -0.6830127018922181881, 0.6830127018922202975, -0.2588190451025214056 ) ) ;
#103657=ORIENTED_EDGE ( 'NONE', *, *, #89284, .T. ) ;
#103658=LINE ( 'NONE', #113848, #59808 ) ;
#103659=VERTEX_POINT ( 'NONE', #130744 ) ;
#103661=ORIENTED_EDGE ( 'NONE', *, *, #133245, .T. ) ;
#103662=VERTEX_POINT ( 'NONE', #8189 ) ;
#103663=ADVANCED_FACE ( 'NONE', ( #52429 ), #117661, .F. ) ;
#103664=EDGE_CURVE ( 'NONE', #98656, #133910, #131442, .T. ) ;
#103666=VERTEX_POINT ( 'NONE', #108209 ) ;
#103667=PLANE ( 'NONE',  #13641 ) ;
#103668=CARTESIAN_POINT ( 'NONE',  ( 0.000000000000000000, 0.000000000000000000, 5.000000000000000000 ) ) ;
#103669=FACE_OUTER_BOUND ( 'NONE', #104058, .T. ) ;
#103671=VERTEX_POINT ( 'NONE', #133587 ) ;
#103673=CARTESIAN_POINT ( 'NONE',  ( -9.299744871391588674, -27.71228299555212971, 4.000000000000000000 ) ) ;
#103674=EDGE_CURVE ( 'NONE', #113044, #42047, #88662, .T. ) ;
#103675=CARTESIAN_POINT ( 'NONE',  ( 0.000000000000000000, 0.000000000000000000, 5.000000000000000000 ) ) ;
#103676=FACE_OUTER_BOUND ( 'NONE', #138652, .T. ) ;
#103677=LINE ( 'NONE', #136330, #4244 ) ;
#103678=LINE ( 'NONE', #16697, #81828 ) ;
#103680=ORIENTED_EDGE ( 'NONE', *, *, #57280, .F. ) ;
#103682=EDGE_LOOP ( 'NONE', ( #65631, #92994, #34622, #29278 ) ) ;
#103683=FACE_OUTER_BOUND ( 'NONE', #83929, .T. ) ;
#103684=ADVANCED_FACE ( 'NONE', ( #66193 ), #12495, .F. ) ;
#103685=ORIENTED_EDGE ( 'NONE', *, *, #85773, .F. ) ;
#103686=ORIENTED_EDGE ( 'NONE', *, *, #14020, .T. ) ;
#103687=CARTESIAN_POINT ( 'NONE',  ( 33.48921356237309510, -27.52281430457078670, 5.000000000000000000 ) ) ;
#103688=LINE ( 'NONE', #61672, #8649 ) ;
#103689=CARTESIAN_POINT ( 'NONE',  ( 6.654944837453786732, 5.259292476615669010, 12.77922209995895209 ) ) ;
#103690=VECTOR ( 'NONE', #97615, 1000.000000000000227 ) ;
#103691=LINE ( 'NONE', #81285, #53229 ) ;
#103694=EDGE_CURVE ( 'NONE', #19810, #7159, #35735, .T. ) ;
#103695=VERTEX_POINT ( 'NONE', #69053 ) ;
#103697=CARTESIAN_POINT ( 'NONE',  ( -1.828169399223509517, 12.75929247661558819, 4.000000000000000000 ) ) ;
#103699=VERTEX_POINT ( 'NONE', #87923 ) ;
#103701=CARTESIAN_POINT ( 'NONE',  ( -19.49999999999986500, -8.568876922607721269, 4.000000000000000000 ) ) ;
#103702=PLANE ( 'NONE',  #90625 ) ;
#103703=DIRECTION ( 'NONE',  ( -0.000000000000000000, -0.3543493200069152693, 0.9351131265310292928 ) ) ;
#103704=ORIENTED_EDGE ( 'NONE', *, *, #138269, .T. ) ;
#103705=EDGE_CURVE ( 'NONE', #46538, #18761, #77084, .T. ) ;
#103706=ORIENTED_EDGE ( 'NONE', *, *, #99829, .T. ) ;
#103707=DIRECTION ( 'NONE',  ( -0.7071067811865487940, 0.7071067811865463515, -0.000000000000000000 ) ) ;
#103709=PLANE ( 'NONE',  #69520 ) ;
#103710=PLANE ( 'NONE',  #99674 ) ;
#103712=DIRECTION ( 'NONE',  ( 0.7071067811865487940, -0.7071067811865463515, 0.000000000000000000 ) ) ;
#103713=DIRECTION ( 'NONE',  ( 0.6830127018922181881, 0.6830127018922202975, -0.2588190451025214056 ) ) ;
#103715=ORIENTED_EDGE ( 'NONE', *, *, #56477, .F. ) ;
#103716=EDGE_CURVE ( 'NONE', #43122, #32117, #135041, .T. ) ;
#103717=DIRECTION ( 'NONE',  ( 0.7071067811865487940, 0.7071067811865463515, -0.000000000000000000 ) ) ;
#103718=EDGE_CURVE ( 'NONE', #48874, #39354, #43709, .T. ) ;
#103719=PLANE ( 'NONE',  #67336 ) ;
#103721=ORIENTED_EDGE ( 'NONE', *, *, #34340, .T. ) ;
#103722=CARTESIAN_POINT ( 'NONE',  ( -33.18398860626899705, 28.73617430169810305, 5.000000000000000000 ) ) ;
#103723=AXIS2_PLACEMENT_3D ( 'NONE', #72410, #104981, #15782 ) ;
#103726=ORIENTED_EDGE ( 'NONE', *, *, #100053, .F. ) ;
#103727=VECTOR ( 'NONE', #27901, 1000.000000000000000 ) ;
#103729=VERTEX_POINT ( 'NONE', #132168 ) ;
#103730=ORIENTED_EDGE ( 'NONE', *, *, #96770, .T. ) ;
#103732=LINE ( 'NONE', #61029, #94647 ) ;
#103733=VECTOR ( 'NONE', #94058, 999.9999999999998863 ) ;
#103734=EDGE_LOOP ( 'NONE', ( #3032, #38562, #93363, #108320 ) ) ;
#103736=VECTOR ( 'NONE', #133320, 1000.000000000000000 ) ;
#103737=CARTESIAN_POINT ( 'NONE',  ( 5.510786437626906675, -27.52281430457051314, 5.000000000000000000 ) ) ;
#103738=DIRECTION ( 'NONE',  ( 0.7071067811865487940, 0.7071067811865463515, -0.000000000000000000 ) ) ;
#103739=ORIENTED_EDGE ( 'NONE', *, *, #94860, .T. ) ;
#103740=ADVANCED_FACE ( 'NONE', ( #54603 ), #68361, .T. ) ;
#103741=CARTESIAN_POINT ( 'NONE',  ( 14.67183060077638324, 20.25929247661552779, 4.000000000000000000 ) ) ;
#103742=CARTESIAN_POINT ( 'NONE',  ( 42.29974487139158157, -27.71228299555235708, 4.000000000000000000 ) ) ;
#103743=CARTESIAN_POINT ( 'NONE',  ( 36.29974487139159578, -27.71228299555231445, 4.000000000000000000 ) ) ;
#103745=CARTESIAN_POINT ( 'NONE',  ( 60.29974487139158867, -27.71228299555248142, 4.000000000000000000 ) ) ;
#103749=DIRECTION ( 'NONE',  ( -0.7071067811865486830, -0.7071067811865464625, 0.000000000000000000 ) ) ;
#103750=EDGE_LOOP ( 'NONE', ( #119316, #130752, #109616 ) ) ;
#103751=VERTEX_POINT ( 'NONE', #57469 ) ;
#103752=ORIENTED_EDGE ( 'NONE', *, *, #41882, .T. ) ;
#103755=VERTEX_POINT ( 'NONE', #55314 ) ;
#103758=AXIS2_PLACEMENT_3D ( 'NONE', #100757, #89864, #91332 ) ;
#103759=CARTESIAN_POINT ( 'NONE',  ( -17.99451991528748351, 28.92564299267950645, 4.000000000000000000 ) ) ;
#103760=ORIENTED_EDGE ( 'NONE', *, *, #114029, .F. ) ;
#103762=CARTESIAN_POINT ( 'NONE',  ( 24.48921356237309510, -27.52281430457072631, 5.000000000000000000 ) ) ;
#103764=CARTESIAN_POINT ( 'NONE',  ( 15.00548008471250228, 28.92564299267927552, 4.000000000000000000 ) ) ;
#103765=DIRECTION ( 'NONE',  ( 1.000000000000000000, 0.000000000000000000, 0.000000000000000000 ) ) ;
#103767=ORIENTED_EDGE ( 'NONE', *, *, #87166, .T. ) ;
#103769=CARTESIAN_POINT ( 'NONE',  ( -25.49999999999982236, 15.43112307739203182, 4.000000000000000000 ) ) ;
#103770=CARTESIAN_POINT ( 'NONE',  ( -30.70701326429283640, -21.74070752338405654, 4.999753212805224223 ) ) ;
#103773=CARTESIAN_POINT ( 'NONE',  ( 17.58838509405156358, 22.22499999999999787, 4.777194822843813249 ) ) ;
#103774=DIRECTION ( 'NONE',  ( 0.7071067811865486830, -0.7071067811865464625, -0.000000000000000000 ) ) ;
#103776=DIRECTION ( 'NONE',  ( 0.7071067811865487940, -0.7071067811865463515, 0.000000000000000000 ) ) ;
#103777=EDGE_CURVE ( 'NONE', #63299, #46769, #22630, .T. ) ;
#103778=LINE ( 'NONE', #137884, #71603 ) ;
#103780=VERTEX_POINT ( 'NONE', #891 ) ;
#103782=ORIENTED_EDGE ( 'NONE', *, *, #135199, .T. ) ;
#103785=LINE ( 'NONE', #82106, #47876 ) ;
#103786=ORIENTED_EDGE ( 'NONE', *, *, #139305, .F. ) ;
#103787=VECTOR ( 'NONE', #4313, 1000.000000000000000 ) ;
#103788=CARTESIAN_POINT ( 'NONE',  ( 1.499999999999993561, 18.05218569542898521, 5.000000000000000000 ) ) ;
#103789=FACE_OUTER_BOUND ( 'NONE', #98668, .T. ) ;
#103790=AXIS2_PLACEMENT_3D ( 'NONE', #43163, #121407, #21401 ) ;
#103791=DIRECTION ( 'NONE',  ( -0.7071067811865486830, -0.7071067811865464625, -0.000000000000000000 ) ) ;
#103793=ORIENTED_EDGE ( 'NONE', *, *, #28449, .T. ) ;
#103794=CARTESIAN_POINT ( 'NONE',  ( -25.17183060077629975, 6.759292476615647693, 4.000000000000000000 ) ) ;
#103795=EDGE_LOOP ( 'NONE', ( #82409, #44933, #89686, #33121 ) ) ;
#103797=CARTESIAN_POINT ( 'NONE',  ( 2.207106781186528810, 15.75929247661555443, 5.000000000000000000 ) ) ;
#103798=DIRECTION ( 'NONE',  ( 0.6830127018922180770, -0.6830127018922204085, -0.2588190451025213501 ) ) ;
#103801=ORIENTED_EDGE ( 'NONE', *, *, #4699, .T. ) ;
#103803=CARTESIAN_POINT ( 'NONE',  ( 34.92460739249803225, 21.74787736706806029, 4.224371856075157972 ) ) ;
#103804=LINE ( 'NONE', #48757, #138035 ) ;
#103805=DIRECTION ( 'NONE',  ( -0.7071067811865487940, 0.7071067811865463515, 0.000000000000000000 ) ) ;
#103807=ORIENTED_EDGE ( 'NONE', *, *, #108419, .T. ) ;
#103809=DIRECTION ( 'NONE',  ( 0.6830127018922180770, -0.6830127018922204085, -0.2588190451025213501 ) ) ;
#103810=ORIENTED_EDGE ( 'NONE', *, *, #109471, .F. ) ;
#103811=ORIENTED_EDGE ( 'NONE', *, *, #57502, .T. ) ;
#103812=FACE_OUTER_BOUND ( 'NONE', #80432, .T. ) ;
#103813=VERTEX_POINT ( 'NONE', #89355 ) ;
#103814=PLANE ( 'NONE',  #72031 ) ;
#103815=VERTEX_POINT ( 'NONE', #101651 ) ;
#103817=ADVANCED_FACE ( 'NONE', ( #160 ), #78488, .F. ) ;
#103818=VECTOR ( 'NONE', #113482, 1000.000000000000000 ) ;
#103819=VECTOR ( 'NONE', #7965, 1000.000000000000227 ) ;
#103821=DIRECTION ( 'NONE',  ( 0.7071067811865486830, -0.7071067811865464625, -0.000000000000000000 ) ) ;
#103823=FACE_BOUND ( 'NONE', #141028, .T. ) ;
#103824=LINE ( 'NONE', #116163, #8581 ) ;
#103825=EDGE_CURVE ( 'NONE', #90791, #120068, #67641, .T. ) ;
#103826=ADVANCED_FACE ( 'NONE', ( #46626 ), #134303, .F. ) ;
#103827=CARTESIAN_POINT ( 'NONE',  ( -15.64318742751728841, -20.24070752338407075, 21.22881796311208902 ) ) ;
#103830=VECTOR ( 'NONE', #104410, 1000.000000000000000 ) ;
#103832=FACE_OUTER_BOUND ( 'NONE', #68153, .T. ) ;
#103833=ORIENTED_EDGE ( 'NONE', *, *, #49089, .F. ) ;
#103834=EDGE_CURVE ( 'NONE', #132228, #32191, #3048, .T. ) ;
#103835=EDGE_CURVE ( 'NONE', #79341, #120024, #16789, .T. ) ;
#103836=VERTEX_POINT ( 'NONE', #136418 ) ;
#103838=ORIENTED_EDGE ( 'NONE', *, *, #101227, .T. ) ;
#103839=CARTESIAN_POINT ( 'NONE',  ( -11.91685193227062101, 21.75929247661549581, 7.311836541448024640 ) ) ;
#103840=PLANE ( 'NONE',  #65795 ) ;
#103841=EDGE_CURVE ( 'NONE', #67478, #91367, #15327, .T. ) ;
#103842=ORIENTED_EDGE ( 'NONE', *, *, #34574, .F. ) ;
#103844=VECTOR ( 'NONE', #5311, 1000.000000000000227 ) ;
#103845=EDGE_CURVE ( 'NONE', #108755, #141993, #104506, .T. ) ;
#103846=EDGE_CURVE ( 'NONE', #99982, #64348, #82091, .T. ) ;
#103847=CARTESIAN_POINT ( 'NONE',  ( -21.16809626817622103, 8.755558144015518351, 4.000000000000000000 ) ) ;
#103848=DIRECTION ( 'NONE',  ( -0.000000000000000000, 0.000000000000000000, 1.000000000000000000 ) ) ;
#103851=LINE ( 'NONE', #72009, #138851 ) ;
#103852=VERTEX_POINT ( 'NONE', #26251 ) ;
#103853=AXIS2_PLACEMENT_3D ( 'NONE', #1569, #58182, #101628 ) ;
#103854=ORIENTED_EDGE ( 'NONE', *, *, #39678, .F. ) ;
#103856=CARTESIAN_POINT ( 'NONE',  ( 14.54487008052911534, -0.7407075233842805861, 4.335043535661647240 ) ) ;
#103857=DIRECTION ( 'NONE',  ( -0.7071067811865487940, 0.7071067811865463515, 0.000000000000000000 ) ) ;
#103858=VERTEX_POINT ( 'NONE', #4411 ) ;
#103859=AXIS2_PLACEMENT_3D ( 'NONE', #117829, #6910, #19267 ) ;
#103861=EDGE_LOOP ( 'NONE', ( #112024, #112652, #60104, #22298 ) ) ;
#103863=VERTEX_POINT ( 'NONE', #126964 ) ;
#103864=DIRECTION ( 'NONE',  ( -0.000000000000000000, -0.000000000000000000, 1.000000000000000000 ) ) ;
#103866=VERTEX_POINT ( 'NONE', #38551 ) ;
#103867=VECTOR ( 'NONE', #1406, 1000.000000000000227 ) ;
#103868=CARTESIAN_POINT ( 'NONE',  ( -8.277185695429338352, -21.72500000000000142, 5.000000000000000000 ) ) ;
#103869=EDGE_CURVE ( 'NONE', #89522, #1245, #47343, .T. ) ;
#103871=DIRECTION ( 'NONE',  ( 0.6830127018922180770, -0.6830127018922204085, -0.2588190451025213501 ) ) ;
#103873=PLANE ( 'NONE',  #132938 ) ;
#103875=FACE_OUTER_BOUND ( 'NONE', #22780, .T. ) ;
#103877=EDGE_CURVE ( 'NONE', #98193, #9777, #115344, .T. ) ;
#103879=VECTOR ( 'NONE', #77907, 1000.000000000000227 ) ;
#103880=DIRECTION ( 'NONE',  ( -0.000000000000000000, 0.3543493200069153248, 0.9351131265310292928 ) ) ;
#103881=ORIENTED_EDGE ( 'NONE', *, *, #104943, .T. ) ;
#103882=DIRECTION ( 'NONE',  ( 0.3543493200069162685, -0.000000000000000000, -0.9351131265310288487 ) ) ;
#103883=VERTEX_POINT ( 'NONE', #127712 ) ;
#103884=DIRECTION ( 'NONE',  ( 1.000000000000000000, 0.000000000000000000, 0.000000000000000000 ) ) ;
#103885=LINE ( 'NONE', #27061, #56177 ) ;
#103887=ORIENTED_EDGE ( 'NONE', *, *, #66793, .T. ) ;
#103888=LINE ( 'NONE', #4532, #38969 ) ;
#103889=EDGE_CURVE ( 'NONE', #49004, #71242, #92190, .T. ) ;
#103890=EDGE_CURVE ( 'NONE', #56792, #61837, #25511, .T. ) ;
#103891=CARTESIAN_POINT ( 'NONE',  ( -24.48921356237309510, -27.52281430457072631, 5.000000000000000000 ) ) ;
#103893=CARTESIAN_POINT ( 'NONE',  ( -42.18398860626899705, 28.73617430169816700, 5.000000000000000000 ) ) ;
#103894=ORIENTED_EDGE ( 'NONE', *, *, #14709, .F. ) ;
#103895=CARTESIAN_POINT ( 'NONE',  ( -32.99999999999976552, -15.41253812416059787, 4.000000000000000000 ) ) ;
#103896=CARTESIAN_POINT ( 'NONE',  ( 34.92499999999998295, -20.24070752338406720, 4.255531930566162302 ) ) ;
#103897=EDGE_CURVE ( 'NONE', #117130, #84461, #53854, .T. ) ;
#103899=EDGE_CURVE ( 'NONE', #131176, #83686, #69787, .T. ) ;
#103900=CARTESIAN_POINT ( 'NONE',  ( -22.49999999999983302, 16.08746187583907528, 4.000000000000000000 ) ) ;
#103901=FACE_OUTER_BOUND ( 'NONE', #108470, .T. ) ;
#103902=ORIENTED_EDGE ( 'NONE', *, *, #41705, .T. ) ;
#103903=ORIENTED_EDGE ( 'NONE', *, *, #37538, .F. ) ;
#103904=DIRECTION ( 'NONE',  ( -0.7071067811865487940, 0.7071067811865463515, 0.000000000000000000 ) ) ;
#103907=CARTESIAN_POINT ( 'NONE',  ( 38.35681257248239007, -20.24070752338406365, 21.22881796311221336 ) ) ;
#103908=LINE ( 'NONE', #4557, #64633 ) ;
#103909=DIRECTION ( 'NONE',  ( -0.7071067811865487940, 0.7071067811865463515, -0.000000000000000000 ) ) ;
#103913=DIRECTION ( 'NONE',  ( -0.6830127018922181881, 0.6830127018922202975, -0.2588190451025214056 ) ) ;
#103915=LINE ( 'NONE', #90211, #117644 ) ;
#103917=ORIENTED_EDGE ( 'NONE', *, *, #140298, .F. ) ;
#103919=EDGE_CURVE ( 'NONE', #84037, #10400, #116092, .T. ) ;
#103920=ORIENTED_EDGE ( 'NONE', *, *, #64758, .F. ) ;
#103921=LINE ( 'NONE', #136568, #32701 ) ;
#103922=ORIENTED_EDGE ( 'NONE', *, *, #107053, .F. ) ;
#103924=CARTESIAN_POINT ( 'NONE',  ( -20.81601139373100295, 28.73617430169773002, 5.000000000000000000 ) ) ;
#103925=AXIS2_PLACEMENT_3D ( 'NONE', #106159, #87303, #6830 ) ;
#103926=AXIS2_PLACEMENT_3D ( 'NONE', #22142, #67107, #1099 ) ;
#103929=VECTOR ( 'NONE', #68944, 1000.000000000000000 ) ;
#103930=CARTESIAN_POINT ( 'NONE',  ( 14.70025512860841133, -27.71228299555195917, 4.000000000000000000 ) ) ;
#103931=ADVANCED_FACE ( 'NONE', ( #137154 ), #5880, .T. ) ;
#103932=DIRECTION ( 'NONE',  ( -0.7071067811865486830, -0.7071067811865464625, -0.000000000000000000 ) ) ;
#103933=VERTEX_POINT ( 'NONE', #50149 ) ;
#103934=EDGE_CURVE ( 'NONE', #42625, #74781, #70514, .T. ) ;
#103935=CARTESIAN_POINT ( 'NONE',  ( -28.49999999999979750, 5.696342897626483825, -7.587980461218466033 ) ) ;
#103936=DIRECTION ( 'NONE',  ( -0.3543493200069162685, -0.000000000000000000, -0.9351131265310288487 ) ) ;
#103938=VECTOR ( 'NONE', #127677, 1000.000000000000227 ) ;
#103939=DIRECTION ( 'NONE',  ( -0.7071067811865486830, -0.7071067811865464625, 0.000000000000000000 ) ) ;
#103940=( BOUNDED_CURVE ( )  B_SPLINE_CURVE ( 3, ( #60285, #116052, #94304, #27617 ),
 .UNSPECIFIED., .F., .T. ) 
 B_SPLINE_CURVE_WITH_KNOTS ( ( 4, 4 ),
 ( 5.920967161967927161, 7.341195215986652478 ),
 .UNSPECIFIED. ) 
 CURVE ( )  GEOMETRIC_REPRESENTATION_ITEM ( )  RATIONAL_B_SPLINE_CURVE ( ( 1.000000000000000000, 0.8388583629366581640, 0.8388583629366581640, 1.000000000000000000 ) ) 
 REPRESENTATION_ITEM ( '' )  );
#103941=LINE ( 'NONE', #47506, #82758 ) ;
#103944=ORIENTED_EDGE ( 'NONE', *, *, #106167, .T. ) ;
#103945=ORIENTED_EDGE ( 'NONE', *, *, #80012, .T. ) ;
#103947=PLANE ( 'NONE',  #123497 ) ;
#103948=PLANE ( 'NONE',  #138894 ) ;
#103949=DIRECTION ( 'NONE',  ( -0.7071067811865487940, 0.7071067811865463515, -0.000000000000000000 ) ) ;
#103950=AXIS2_PLACEMENT_3D ( 'NONE', #81882, #60108, #105006 ) ;
#103952=ORIENTED_EDGE ( 'NONE', *, *, #64953, .F. ) ;
#103953=EDGE_CURVE ( 'NONE', #120446, #25807, #126271, .T. ) ;
#103956=EDGE_CURVE ( 'NONE', #86807, #123482, #95774, .T. ) ;
#103959=FACE_OUTER_BOUND ( 'NONE', #113418, .T. ) ;
#103960=ORIENTED_EDGE ( 'NONE', *, *, #21229, .F. ) ;
#103961=ORIENTED_EDGE ( 'NONE', *, *, #61608, .F. ) ;
#103962=VECTOR ( 'NONE', #139696, 1000.000000000000227 ) ;
#103963=AXIS2_PLACEMENT_3D ( 'NONE', #97528, #22786, #109840 ) ;
#103964=CARTESIAN_POINT ( 'NONE',  ( 27.70701326429285061, -21.74070752338406365, 4.999753212805213565 ) ) ;
#103965=FACE_OUTER_BOUND ( 'NONE', #3468, .T. ) ;
#103966=AXIS2_PLACEMENT_3D ( 'NONE', #66509, #67215, #46209 ) ;
#103968=EDGE_CURVE ( 'NONE', #10069, #130801, #19642, .T. ) ;
#103969=CARTESIAN_POINT ( 'NONE',  ( -17.99999999999986855, -16.60178936734450161, 0.8616154019347073145 ) ) ;
#103970=CARTESIAN_POINT ( 'NONE',  ( -12.79289321881336683, 3.759292476615678336, 5.000000000000000000 ) ) ;
#103971=ORIENTED_EDGE ( 'NONE', *, *, #97333, .F. ) ;
#103973=DIRECTION ( 'NONE',  ( -0.000000000000000000, -0.3543493200069152693, 0.9351131265310292928 ) ) ;
#103974=CARTESIAN_POINT ( 'NONE',  ( 27.08314806772914451, 21.75929247661549581, 7.311836541448114346 ) ) ;
#103975=VECTOR ( 'NONE', #117146, 1000.000000000000000 ) ;
#103976=LINE ( 'NONE', #135239, #94721 ) ;
#103977=VECTOR ( 'NONE', #72222, 1000.000000000000227 ) ;
#103978=EDGE_LOOP ( 'NONE', ( #129705, #134243, #28260, #115884 ) ) ;
#103979=VERTEX_POINT ( 'NONE', #119639 ) ;
#103981=DIRECTION ( 'NONE',  ( -0.7071067811865486830, 0.7071067811865464625, 0.000000000000000000 ) ) ;
#103983=CARTESIAN_POINT ( 'NONE',  ( -18.32816939922340183, -6.740707523384207533, 4.000000000000000000 ) ) ;
#103984=ORIENTED_EDGE ( 'NONE', *, *, #82284, .F. ) ;
#103985=ORIENTED_EDGE ( 'NONE', *, *, #141435, .T. ) ;
#103986=VECTOR ( 'NONE', #67598, 1000.000000000000227 ) ;
#103987=FACE_OUTER_BOUND ( 'NONE', #38785, .T. ) ;
#103988=FACE_OUTER_BOUND ( 'NONE', #14522, .T. ) ;
#103989=ORIENTED_EDGE ( 'NONE', *, *, #33492, .F. ) ;
#103990=CARTESIAN_POINT ( 'NONE',  ( 34.42499999999998295, 13.54139925780190445, 5.000000000000000000 ) ) ;
#103992=CARTESIAN_POINT ( 'NONE',  ( 0.000000000000000000, 0.000000000000000000, 5.000000000000000000 ) ) ;
#103993=CARTESIAN_POINT ( 'NONE',  ( -3.792893218813427669, -2.240707523384264377, 5.000000000000000000 ) ) ;
#103994=FACE_BOUND ( 'NONE', #110648, .T. ) ;
#103995=CARTESIAN_POINT ( 'NONE',  ( -33.48921356237309510, -27.52281430457078670, 5.000000000000000000 ) ) ;
#103996=EDGE_CURVE ( 'NONE', #100892, #90194, #105912, .T. ) ;
#103997=DIRECTION ( 'NONE',  ( 0.7071067811865487940, -0.7071067811865463515, 0.000000000000000000 ) ) ;
#103998=CARTESIAN_POINT ( 'NONE',  ( 44.99451991528749772, 28.92564299267969474, 4.000000000000000000 ) ) ;
#104000=CARTESIAN_POINT ( 'NONE',  ( 34.21321903303337564, 12.75929247661558641, 10.29404684609043308 ) ) ;
#104002=ORIENTED_EDGE ( 'NONE', *, *, #9853, .F. ) ;
#104003=ADVANCED_FACE ( 'NONE', ( #29098 ), #116813, .F. ) ;
#104006=EDGE_LOOP ( 'NONE', ( #70187, #121609, #139819, #3519 ) ) ;
#104007=EDGE_CURVE ( 'NONE', #60798, #79691, #50854, .T. ) ;
#104008=LINE ( 'NONE', #57713, #76675 ) ;
#104009=EDGE_CURVE ( 'NONE', #30305, #63170, #85598, .T. ) ;
#104010=DIRECTION ( 'NONE',  ( -0.7071067811865486830, -0.7071067811865464625, 0.000000000000000000 ) ) ;
#104012=LINE ( 'NONE', #51112, #77223 ) ;
#104013=ORIENTED_EDGE ( 'NONE', *, *, #120874, .F. ) ;
#104014=DIRECTION ( 'NONE',  ( 0.7071067811865487940, 0.7071067811865463515, 0.000000000000000000 ) ) ;
#104016=EDGE_CURVE ( 'NONE', #33632, #15104, #61750, .T. ) ;
#104017=CARTESIAN_POINT ( 'NONE',  ( -9.084913231937559175, -12.74070752338414891, 18.74364270924352027 ) ) ;
#104018=CARTESIAN_POINT ( 'NONE',  ( -5.293876922608010460, 22.22500000000000142, 4.000000000000000000 ) ) ;
#104019=DIRECTION ( 'NONE',  ( 0.7071067811865487940, 0.7071067811865463515, 0.000000000000000000 ) ) ;
#104020=PLANE ( 'NONE',  #117885 ) ;
#104022=VECTOR ( 'NONE', #132280, 1000.000000000000000 ) ;
#104023=VECTOR ( 'NONE', #33715, 1000.000000000000227 ) ;
#104024=CARTESIAN_POINT ( 'NONE',  ( -34.92500000000001137, -9.281509562795667634, 4.759050581649335143 ) ) ;
#104025=VECTOR ( 'NONE', #39861, 1000.000000000000000 ) ;
#104026=VERTEX_POINT ( 'NONE', #84902 ) ;
#104028=FACE_OUTER_BOUND ( 'NONE', #88693, .T. ) ;
#104029=VECTOR ( 'NONE', #127394, 1000.000000000000227 ) ;
#104030=EDGE_CURVE ( 'NONE', #70917, #135458, #108400, .T. ) ;
#104031=EDGE_LOOP ( 'NONE', ( #26673, #121623, #53060, #137735 ) ) ;
#104032=VERTEX_POINT ( 'NONE', #108757 ) ;
#104033=ADVANCED_FACE ( 'NONE', ( #86350 ), #29792, .F. ) ;
#104034=ORIENTED_EDGE ( 'NONE', *, *, #21382, .T. ) ;
#104036=EDGE_LOOP ( 'NONE', ( #77398, #73538, #120948, #66979 ) ) ;
#104037=VECTOR ( 'NONE', #41186, 1000.000000000000000 ) ;
#104038=EDGE_CURVE ( 'NONE', #31242, #74888, #97164, .T. ) ;
#104039=VECTOR ( 'NONE', #33536, 1000.000000000000000 ) ;
#104041=VERTEX_POINT ( 'NONE', #131266 ) ;
#104042=DIRECTION ( 'NONE',  ( -0.6830127018922181881, 0.6830127018922202975, -0.2588190451025214056 ) ) ;
#104043=ORIENTED_EDGE ( 'NONE', *, *, #49080, .T. ) ;
#104045=AXIS2_PLACEMENT_3D ( 'NONE', #44815, #131779, #99107 ) ;
#104046=DIRECTION ( 'NONE',  ( -1.000000000000000000, 0.000000000000000000, -0.000000000000000000 ) ) ;
#104047=DIRECTION ( 'NONE',  ( -0.6830127018922180770, -0.6830127018922204085, -0.2588190451025213501 ) ) ;
#104048=VERTEX_POINT ( 'NONE', #74772 ) ;
#104050=FACE_OUTER_BOUND ( 'NONE', #80808, .T. ) ;
#104051=CARTESIAN_POINT ( 'NONE',  ( -22.17183060077632106, -11.24070752338416845, 4.000000000000000000 ) ) ;
#104052=ORIENTED_EDGE ( 'NONE', *, *, #85357, .F. ) ;
#104054=LINE ( 'NONE', #49741, #136135 ) ;
#104055=ORIENTED_EDGE ( 'NONE', *, *, #87479, .T. ) ;
#104056=ORIENTED_EDGE ( 'NONE', *, *, #126256, .F. ) ;
#104058=EDGE_LOOP ( 'NONE', ( #19362, #18791, #120029, #65705 ) ) ;
#104059=EDGE_CURVE ( 'NONE', #121778, #131245, #133446, .T. ) ;
#104060=FACE_OUTER_BOUND ( 'NONE', #113708, .T. ) ;
#104062=VECTOR ( 'NONE', #135032, 1000.000000000000000 ) ;
#104064=VECTOR ( 'NONE', #54419, 999.9999999999998863 ) ;
#104066=CARTESIAN_POINT ( 'NONE',  ( -84.29974487139159578, -27.71228299555264840, 4.000000000000000000 ) ) ;
#104067=CARTESIAN_POINT ( 'NONE',  ( 33.18398860626899705, 28.73617430169810305, 5.000000000000000000 ) ) ;
#104068=ORIENTED_EDGE ( 'NONE', *, *, #91441, .T. ) ;
#104069=VECTOR ( 'NONE', #77963, 1000.000000000000000 ) ;
#104070=LINE ( 'NONE', #83818, #107290 ) ;
#104073=DIRECTION ( 'NONE',  ( -0.000000000000000000, 0.000000000000000000, 1.000000000000000000 ) ) ;
#104077=ORIENTED_EDGE ( 'NONE', *, *, #108593, .F. ) ;
#104078=ADVANCED_FACE ( 'NONE', ( #121091 ), #21060, .T. ) ;
#104079=ORIENTED_EDGE ( 'NONE', *, *, #38682, .F. ) ;
#104086=DIRECTION ( 'NONE',  ( 0.7071067811865487940, -0.7071067811865463515, 0.000000000000000000 ) ) ;
#104088=DIRECTION ( 'NONE',  ( -0.7071067811865486830, -0.7071067811865464625, 0.000000000000000000 ) ) ;
#104089=LINE ( 'NONE', #106230, #46079 ) ;
#104090=LINE ( 'NONE', #137479, #111224 ) ;
#104092=CARTESIAN_POINT ( 'NONE',  ( -17.99451991528748351, 28.92564299267950645, 4.000000000000000000 ) ) ;
#104093=CARTESIAN_POINT ( 'NONE',  ( 29.24139925780183091, 21.72500000000000853, 5.000000000000000000 ) ) ;
#104094=ORIENTED_EDGE ( 'NONE', *, *, #35498, .T. ) ;
#104097=LINE ( 'NONE', #36044, #127062 ) ;
#104098=CARTESIAN_POINT ( 'NONE',  ( 34.42499999999998295, -16.45860074219779889, 5.000000000000000000 ) ) ;
#104099=ORIENTED_EDGE ( 'NONE', *, *, #64213, .F. ) ;
#104100=EDGE_CURVE ( 'NONE', #16952, #3281, #1432, .T. ) ;
#104101=PLANE ( 'NONE',  #95003 ) ;
#104102=DIRECTION ( 'NONE',  ( -0.7071067811865486830, -0.7071067811865464625, 0.000000000000000000 ) ) ;
#104103=ORIENTED_EDGE ( 'NONE', *, *, #69191, .T. ) ;
#104104=DIRECTION ( 'NONE',  ( 0.7071067811865487940, -0.7071067811865463515, 0.000000000000000000 ) ) ;
#104105=ORIENTED_EDGE ( 'NONE', *, *, #11729, .T. ) ;
#104106=CARTESIAN_POINT ( 'NONE',  ( -3.005480084712505828, 28.92564299267936079, 4.000000000000000000 ) ) ;
#104110=FACE_OUTER_BOUND ( 'NONE', #128565, .T. ) ;
#104111=FACE_OUTER_BOUND ( 'NONE', #11607, .T. ) ;
#104112=ORIENTED_EDGE ( 'NONE', *, *, #51855, .F. ) ;
#104113=DIRECTION ( 'NONE',  ( -0.7071067811865486830, -0.7071067811865464625, 0.000000000000000000 ) ) ;
#104114=LINE ( 'NONE', #126595, #34571 ) ;
#104117=CARTESIAN_POINT ( 'NONE',  ( -10.49999999999992539, 3.073033219394616378, -6.593910359670993593 ) ) ;
#104118=EDGE_LOOP ( 'NONE', ( #45334, #88180, #31313, #101699 ) ) ;
#104119=DIRECTION ( 'NONE',  ( 0.7071067811865486830, -0.7071067811865464625, -0.000000000000000000 ) ) ;
#104120=ORIENTED_EDGE ( 'NONE', *, *, #119329, .F. ) ;
#104121=ADVANCED_FACE ( 'NONE', ( #121792 ), #89889, .F. ) ;
#104123=CARTESIAN_POINT ( 'NONE',  ( -24.18398860626899705, 28.73617430169804265, 5.000000000000000000 ) ) ;
#104125=CARTESIAN_POINT ( 'NONE',  ( 9.183988606268997046, 28.73617430169793607, 5.000000000000000000 ) ) ;
#104126=CARTESIAN_POINT ( 'NONE',  ( -78.29974487139158157, -27.71228299555260577, 4.000000000000000000 ) ) ;
#104127=ORIENTED_EDGE ( 'NONE', *, *, #128123, .F. ) ;
#104128=VECTOR ( 'NONE', #60651, 1000.000000000000000 ) ;
#104130=DIRECTION ( 'NONE',  ( -0.7071067811865487940, 0.7071067811865463515, -0.000000000000000000 ) ) ;
#104131=VECTOR ( 'NONE', #47424, 1000.000000000000000 ) ;
#104133=DIRECTION ( 'NONE',  ( 0.7071067811865487940, 0.7071067811865463515, 0.000000000000000000 ) ) ;
#104134=ADVANCED_FACE ( 'NONE', ( #120342 ), #65328, .T. ) ;
#104135=CARTESIAN_POINT ( 'NONE',  ( 14.58838509405157602, 22.22500000000000142, 4.777194822843812361 ) ) ;
#104136=CARTESIAN_POINT ( 'NONE',  ( -12.29974487139158512, -27.71228299555214747, 4.000000000000000000 ) ) ;
#104137=ORIENTED_EDGE ( 'NONE', *, *, #27301, .T. ) ;
#104138=CARTESIAN_POINT ( 'NONE',  ( 5.816011393731002066, 28.73617430169783304, 5.000000000000000000 ) ) ;
#104139=DIRECTION ( 'NONE',  ( 0.6830127018922181881, 0.6830127018922202975, -0.2588190451025214056 ) ) ;
#104140=AXIS2_PLACEMENT_3D ( 'NONE', #98279, #84555, #9065 ) ;
#104141=LINE ( 'NONE', #4805, #16855 ) ;
#104143=ORIENTED_EDGE ( 'NONE', *, *, #6687, .F. ) ;
#104145=EDGE_LOOP ( 'NONE', ( #66226, #110638, #55172, #42771 ) ) ;
#104147=ORIENTED_EDGE ( 'NONE', *, *, #62326, .T. ) ;
#104150=VECTOR ( 'NONE', #50137, 1000.000000000000000 ) ;
#104151=DIRECTION ( 'NONE',  ( 0.3543493200069163240, 0.000000000000000000, -0.9351131265310288487 ) ) ;
#104152=DIRECTION ( 'NONE',  ( 0.6830127018922180770, -0.6830127018922204085, -0.2588190451025213501 ) ) ;
#104153=ORIENTED_EDGE ( 'NONE', *, *, #71640, .T. ) ;
#104154=ADVANCED_FACE ( 'NONE', ( #10875 ), #131994, .T. ) ;
#104155=PLANE ( 'NONE',  #97680 ) ;
#104158=VECTOR ( 'NONE', #59799, 999.9999999999998863 ) ;
#104160=EDGE_LOOP ( 'NONE', ( #7350, #142000, #50519, #127097 ) ) ;
#104161=CARTESIAN_POINT ( 'NONE',  ( 17.99451991528748351, 28.92564299267950645, 4.000000000000000000 ) ) ;
#104162=CARTESIAN_POINT ( 'NONE',  ( 34.92499999999998295, -4.298069433178973497, 4.500000000000000888 ) ) ;
#104163=VECTOR ( 'NONE', #127515, 1000.000000000000227 ) ;
#104165=ORIENTED_EDGE ( 'NONE', *, *, #43631, .T. ) ;
#104166=LINE ( 'NONE', #118459, #88636 ) ;
#104168=DIRECTION ( 'NONE',  ( -0.7071067811865486830, 0.7071067811865464625, 0.000000000000000000 ) ) ;
#104169=DIRECTION ( 'NONE',  ( 0.7071067811865486830, -0.7071067811865464625, -0.000000000000000000 ) ) ;
#104170=VECTOR ( 'NONE', #26265, 1000.000000000000000 ) ;
#104171=LINE ( 'NONE', #102072, #59605 ) ;
#104172=DIRECTION ( 'NONE',  ( -0.7071067811865486830, -0.7071067811865464625, 0.000000000000000000 ) ) ;
#104173=LINE ( 'NONE', #91898, #58218 ) ;
#104175=EDGE_CURVE ( 'NONE', #86612, #53081, #67470, .T. ) ;
#104176=VECTOR ( 'NONE', #64106, 1000.000000000000227 ) ;
#104177=ORIENTED_EDGE ( 'NONE', *, *, #63147, .F. ) ;
#104179=EDGE_CURVE ( 'NONE', #25213, #55140, #57308, .T. ) ;
#104181=ADVANCED_FACE ( 'NONE', ( #55872 ), #10185, .F. ) ;
#104182=VECTOR ( 'NONE', #10341, 1000.000000000000000 ) ;
#104183=EDGE_CURVE ( 'NONE', #21250, #20431, #23182, .T. ) ;
#104184=LINE ( 'NONE', #62157, #73358 ) ;
#104185=CARTESIAN_POINT ( 'NONE',  ( -10.49999999999993072, 15.43112307739203182, 4.000000000000000000 ) ) ;
#104186=VERTEX_POINT ( 'NONE', #76180 ) ;
#104188=DIRECTION ( 'NONE',  ( -0.000000000000000000, 0.3543493200069153248, 0.9351131265310292928 ) ) ;
#104189=CARTESIAN_POINT ( 'NONE',  ( 3.989119713460488992, -22.02621442084248216, 4.990779571109224655 ) ) ;
#104190=DIRECTION ( 'NONE',  ( 0.7071067811865487940, -0.7071067811865463515, 0.000000000000000000 ) ) ;
#104191=VECTOR ( 'NONE', #60430, 1000.000000000000000 ) ;
#104192=CARTESIAN_POINT ( 'NONE',  ( 2.816011393730999401, 28.73617430169785436, 5.000000000000000000 ) ) ;
#104193=EDGE_LOOP ( 'NONE', ( #29050, #53856, #82693, #143006 ) ) ;
#104194=DIRECTION ( 'NONE',  ( 0.6830127018922181881, 0.6830127018922202975, -0.2588190451025214056 ) ) ;
#104195=LINE ( 'NONE', #126676, #113548 ) ;
#104196=ADVANCED_FACE ( 'NONE', ( #66038 ), #111661, .F. ) ;
#104197=ORIENTED_EDGE ( 'NONE', *, *, #98504, .T. ) ;
#104198=CARTESIAN_POINT ( 'NONE',  ( 16.88727739707083231, 22.22500000000000142, 24.63360875038745235 ) ) ;
#104201=ORIENTED_EDGE ( 'NONE', *, *, #23323, .F. ) ;
#104202=CARTESIAN_POINT ( 'NONE',  ( -36.48921356237310221, -27.52281430457080802, 5.000000000000000000 ) ) ;
#104203=ORIENTED_EDGE ( 'NONE', *, *, #98984, .T. ) ;
#104204=VERTEX_POINT ( 'NONE', #13030 ) ;
#104206=AXIS2_PLACEMENT_3D ( 'NONE', #72276, #39623, #61396 ) ;
#104207=ORIENTED_EDGE ( 'NONE', *, *, #128914, .F. ) ;
#104208=EDGE_CURVE ( 'NONE', #87694, #21974, #104315, .T. ) ;
#104209=FACE_OUTER_BOUND ( 'NONE', #128235, .T. ) ;
#104210=CARTESIAN_POINT ( 'NONE',  ( 27.70701326429285061, -21.74070752338406365, 4.999753212805213565 ) ) ;
#104211=LINE ( 'NONE', #38989, #112180 ) ;
#104213=CARTESIAN_POINT ( 'NONE',  ( 24.29974487139158867, -27.71228299555223273, 4.000000000000000000 ) ) ;
#104214=DIRECTION ( 'NONE',  ( 0.7071067811865486830, -0.7071067811865464625, -0.000000000000000000 ) ) ;
#104215=DIRECTION ( 'NONE',  ( 0.6830127018922180770, -0.6830127018922204085, -0.2588190451025213501 ) ) ;
#104216=ADVANCED_FACE ( 'NONE', ( #16605 ), #113794, .F. ) ;
#104217=VECTOR ( 'NONE', #54923, 1000.000000000000000 ) ;
#104218=PLANE ( 'NONE',  #63243 ) ;
#104220=VECTOR ( 'NONE', #48595, 1000.000000000000000 ) ;
#104224=DIRECTION ( 'NONE',  ( -0.7071067811865486830, 0.7071067811865464625, 0.000000000000000000 ) ) ;
#104225=CARTESIAN_POINT ( 'NONE',  ( 25.98012225071437342, -17.24070752338409918, 20.23474786156475602 ) ) ;
#104226=VERTEX_POINT ( 'NONE', #70341 ) ;
#104227=VERTEX_POINT ( 'NONE', #15853 ) ;
#104230=CARTESIAN_POINT ( 'NONE',  ( 13.82816939922343558, 15.75929247661555443, 4.000000000000000000 ) ) ;
#104231=AXIS2_PLACEMENT_3D ( 'NONE', #40463, #62211, #142450 ) ;
#104232=AXIS2_PLACEMENT_3D ( 'NONE', #44981, #48491, #15807 ) ;
#104233=VERTEX_POINT ( 'NONE', #69608 ) ;
#104234=VECTOR ( 'NONE', #112153, 1000.000000000000000 ) ;
#104235=PLANE ( 'NONE',  #16627 ) ;
#104236=LINE ( 'NONE', #4900, #101111 ) ;
#104237=DIRECTION ( 'NONE',  ( 0.7071067811865487940, -0.7071067811865463515, 0.000000000000000000 ) ) ;
#104238=DIRECTION ( 'NONE',  ( -0.7071067811865487940, 0.7071067811865463515, -0.000000000000000000 ) ) ;
#104239=EDGE_LOOP ( 'NONE', ( #2522, #21687, #45783, #123684 ) ) ;
#104241=AXIS2_PLACEMENT_3D ( 'NONE', #11585, #63880, #31949 ) ;
#104242=ORIENTED_EDGE ( 'NONE', *, *, #45082, .T. ) ;
#104243=CARTESIAN_POINT ( 'NONE',  ( 34.42499999999998295, -0.02281430457060432127, 5.000000000000000000 ) ) ;
#104244=EDGE_CURVE ( 'NONE', #18293, #123961, #92029, .T. ) ;
#104246=CARTESIAN_POINT ( 'NONE',  ( 5.671830600776434750, -0.7407075233842735917, 4.000000000000000000 ) ) ;
#104247=PLANE ( 'NONE',  #20524 ) ;
#104249=VERTEX_POINT ( 'NONE', #91356 ) ;
#104250=ORIENTED_EDGE ( 'NONE', *, *, #105092, .F. ) ;
#104251=ORIENTED_EDGE ( 'NONE', *, *, #96503, .T. ) ;
#104252=FACE_OUTER_BOUND ( 'NONE', #4767, .T. ) ;
#104253=VECTOR ( 'NONE', #66716, 1000.000000000000227 ) ;
#104255=CARTESIAN_POINT ( 'NONE',  ( 45.48921356237309510, -27.52281430457087197, 5.000000000000000000 ) ) ;
#104256=CARTESIAN_POINT ( 'NONE',  ( -8.207106781186485733, 9.759292476615620160, 5.000000000000000000 ) ) ;
#104257=CARTESIAN_POINT ( 'NONE',  ( -6.084913231937570721, -12.74070752338414891, 18.74364270924352738 ) ) ;
#104258=FACE_OUTER_BOUND ( 'NONE', #86714, .T. ) ;
#104259=VECTOR ( 'NONE', #76040, 999.9999999999998863 ) ;
#104261=CARTESIAN_POINT ( 'NONE',  ( 0.000000000000000000, 0.000000000000000000, 5.000000000000000000 ) ) ;
#104263=DIRECTION ( 'NONE',  ( -0.7071067811865486830, -0.7071067811865464625, 0.000000000000000000 ) ) ;
#104264=DIRECTION ( 'NONE',  ( 0.7071067811865487940, 0.7071067811865463515, 0.000000000000000000 ) ) ;
#104265=VECTOR ( 'NONE', #126269, 1000.000000000000000 ) ;
#104266=ORIENTED_EDGE ( 'NONE', *, *, #76529, .F. ) ;
#104267=LINE ( 'NONE', #84688, #53368 ) ;
#104268=CARTESIAN_POINT ( 'NONE',  ( 2.700255128608413990, -27.71228299555204089, 4.000000000000000000 ) ) ;
#104269=VECTOR ( 'NONE', #106964, 1000.000000000000000 ) ;
#104270=ORIENTED_EDGE ( 'NONE', *, *, #131628, .T. ) ;
#104271=CARTESIAN_POINT ( 'NONE',  ( -3.183988606268992161, 28.73617430169789699, 5.000000000000000000 ) ) ;
#104273=EDGE_LOOP ( 'NONE', ( #12591, #83570, #21516, #40114 ) ) ;
#104274=ADVANCED_FACE ( 'NONE', ( #59448 ), #82594, .T. ) ;
#104277=DIRECTION ( 'NONE',  ( 1.000000000000000000, 0.000000000000000000, 0.000000000000000000 ) ) ;
#104278=CARTESIAN_POINT ( 'NONE',  ( 48.48921356237309510, -27.52281430457089328, 5.000000000000000000 ) ) ;
#104279=ORIENTED_EDGE ( 'NONE', *, *, #62813, .T. ) ;
#104280=ORIENTED_EDGE ( 'NONE', *, *, #16166, .T. ) ;
#104281=FACE_OUTER_BOUND ( 'NONE', #30262, .T. ) ;
#104282=DIRECTION ( 'NONE',  ( 1.000000000000000000, 0.000000000000000000, 0.000000000000000000 ) ) ;
#104284=FACE_OUTER_BOUND ( 'NONE', #56641, .T. ) ;
#104285=VECTOR ( 'NONE', #9797, 999.9999999999998863 ) ;
#104286=CARTESIAN_POINT ( 'NONE',  ( 12.51665438641036054, 22.22500000000000142, 4.500000000000000888 ) ) ;
#104287=LINE ( 'NONE', #3541, #137127 ) ;
#104288=ADVANCED_FACE ( 'NONE', ( #81184 ), #14482, .T. ) ;
#104289=LINE ( 'NONE', #92006, #49470 ) ;
#104290=CARTESIAN_POINT ( 'NONE',  ( -28.49999999999979750, 9.052185695429079360, 5.000000000000000000 ) ) ;
#104292=AXIS2_PLACEMENT_3D ( 'NONE', #119463, #77454, #76734 ) ;
#104294=DIRECTION ( 'NONE',  ( -0.7071067811865487940, 0.7071067811865463515, -0.000000000000000000 ) ) ;
#104295=DIRECTION ( 'NONE',  ( -0.000000000000000000, -0.3543493200069152693, 0.9351131265310292928 ) ) ;
#104296=LINE ( 'NONE', #134113, #13010 ) ;
#104297=ORIENTED_EDGE ( 'NONE', *, *, #42945, .F. ) ;
#104298=ORIENTED_EDGE ( 'NONE', *, *, #50390, .T. ) ;
#104300=ORIENTED_EDGE ( 'NONE', *, *, #118546, .T. ) ;
#104301=ORIENTED_EDGE ( 'NONE', *, *, #69015, .T. ) ;
#104303=CARTESIAN_POINT ( 'NONE',  ( 19.82816939922339472, 15.75929247661555976, 4.000000000000000000 ) ) ;
#104304=CARTESIAN_POINT ( 'NONE',  ( 2.999999999999981792, -7.447814304570750998, 5.000000000000000000 ) ) ;
#104305=AXIS2_PLACEMENT_3D ( 'NONE', #45805, #79166, #79883 ) ;
#104306=PLANE ( 'NONE',  #12999 ) ;
#104307=EDGE_LOOP ( 'NONE', ( #140467, #62264, #7382, #62333 ) ) ;
#104308=DIRECTION ( 'NONE',  ( 0.7071067811865487940, -0.7071067811865463515, 0.000000000000000000 ) ) ;
#104309=CARTESIAN_POINT ( 'NONE',  ( 21.18398860626899349, 28.73617430169802134, 5.000000000000000000 ) ) ;
#104310=CARTESIAN_POINT ( 'NONE',  ( 29.99999999999979039, 16.93112307739200872, 4.000000000000000000 ) ) ;
#104313=EDGE_CURVE ( 'NONE', #120068, #63590, #58027, .T. ) ;
#104314=PLANE ( 'NONE',  #116425 ) ;
#104315=LINE ( 'NONE', #48540, #100658 ) ;
#104317=VECTOR ( 'NONE', #124289, 1000.000000000000227 ) ;
#104318=CARTESIAN_POINT ( 'NONE',  ( 0.000000000000000000, 0.000000000000000000, 5.000000000000000000 ) ) ;
#104319=CARTESIAN_POINT ( 'NONE',  ( 13.00193056682088688, -22.22500000000000142, 4.500000000000000888 ) ) ;
#104320=AXIS2_PLACEMENT_3D ( 'NONE', #39951, #95717, #18860 ) ;
#104321=DIRECTION ( 'NONE',  ( -0.7071067811865487940, 0.7071067811865463515, 0.000000000000000000 ) ) ;
#104322=FACE_OUTER_BOUND ( 'NONE', #56626, .T. ) ;
#104323=ORIENTED_EDGE ( 'NONE', *, *, #70717, .F. ) ;
#104324=ORIENTED_EDGE ( 'NONE', *, *, #92402, .F. ) ;
#104326=( BOUNDED_CURVE ( )  B_SPLINE_CURVE ( 3, ( #99536, #124172, #69097, #77820 ),
 .UNSPECIFIED., .F., .T. ) 
 B_SPLINE_CURVE_WITH_KNOTS ( ( 4, 4 ),
 ( 0.6783063634690165156, 0.7469765549618204714 ),
 .UNSPECIFIED. ) 
 CURVE ( )  GEOMETRIC_REPRESENTATION_ITEM ( )  RATIONAL_B_SPLINE_CURVE ( ( 1.000000000000000000, 0.9996070723374664846, 0.9996070723374664846, 1.000000000000000000 ) ) 
 REPRESENTATION_ITEM ( '' )  );
#104327=ORIENTED_EDGE ( 'NONE', *, *, #136431, .F. ) ;
#104328=EDGE_CURVE ( 'NONE', #26996, #101519, #102227, .T. ) ;
#104329=CARTESIAN_POINT ( 'NONE',  ( -29.20710678118633652, 15.75929247661555443, 5.000000000000000000 ) ) ;
#104331=VECTOR ( 'NONE', #17119, 999.9999999999998863 ) ;
#104333=DIRECTION ( 'NONE',  ( -0.3543493200069162685, -0.000000000000000000, -0.9351131265310288487 ) ) ;
#104334=DIRECTION ( 'NONE',  ( 1.000000000000000000, 0.000000000000000000, 0.000000000000000000 ) ) ;
#104338=ORIENTED_EDGE ( 'NONE', *, *, #823, .T. ) ;
#104339=DIRECTION ( 'NONE',  ( 0.7071067811865487940, 0.7071067811865463515, 0.000000000000000000 ) ) ;
#104340=ORIENTED_EDGE ( 'NONE', *, *, #299, .F. ) ;
#104341=DIRECTION ( 'NONE',  ( -0.7071067811865486830, -0.7071067811865464625, 0.000000000000000000 ) ) ;
#104342=AXIS2_PLACEMENT_3D ( 'NONE', #8148, #130700, #9576 ) ;
#104345=VECTOR ( 'NONE', #50460, 999.9999999999998863 ) ;
#104346=VECTOR ( 'NONE', #106646, 999.9999999999998863 ) ;
#104347=CARTESIAN_POINT ( 'NONE',  ( -15.70679250724064246, 20.25929247661551358, 20.83292124670818524 ) ) ;
#104349=EDGE_LOOP ( 'NONE', ( #115993, #9546, #88858, #45402 ) ) ;
#104350=VERTEX_POINT ( 'NONE', #47175 ) ;
#104351=VERTEX_POINT ( 'NONE', #126789 ) ;
#104353=CARTESIAN_POINT ( 'NONE',  ( 16.17183060077635659, 21.75929247661549937, 4.000000000000000000 ) ) ;
#104355=AXIS2_PLACEMENT_3D ( 'NONE', #69421, #90437, #112898 ) ;
#104357=EDGE_CURVE ( 'NONE', #79591, #142882, #36247, .T. ) ;
#104359=ORIENTED_EDGE ( 'NONE', *, *, #90142, .T. ) ;
#104360=ORIENTED_EDGE ( 'NONE', *, *, #108705, .F. ) ;
#104361=VECTOR ( 'NONE', #37907, 1000.000000000000000 ) ;
#104362=EDGE_CURVE ( 'NONE', #109128, #42329, #3569, .T. ) ;
#104363=DIRECTION ( 'NONE',  ( 0.6830127018922180770, -0.6830127018922204085, -0.2588190451025213501 ) ) ;
#104364=ORIENTED_EDGE ( 'NONE', *, *, #61436, .F. ) ;
#104365=VERTEX_POINT ( 'NONE', #4983 ) ;
#104367=ADVANCED_FACE ( 'NONE', ( #114488 ), #103603, .F. ) ;
#104368=ADVANCED_FACE ( 'NONE', ( #27474 ), #115896, .F. ) ;
#104369=PLANE ( 'NONE',  #132779 ) ;
#104370=AXIS2_PLACEMENT_3D ( 'NONE', #44526, #88726, #90119 ) ;
#104371=VECTOR ( 'NONE', #926, 1000.000000000000000 ) ;
#104372=CARTESIAN_POINT ( 'NONE',  ( -17.99451991528748351, 28.92564299267950645, 4.000000000000000000 ) ) ;
#104373=CARTESIAN_POINT ( 'NONE',  ( 21.88339156388719431, -2.079482862307782121, 4.335713449946893228 ) ) ;
#104374=VERTEX_POINT ( 'NONE', #6397 ) ;
#104375=CARTESIAN_POINT ( 'NONE',  ( 26.29289321881326558, 17.25929247661554200, 5.000000000000000000 ) ) ;
#104376=VECTOR ( 'NONE', #111545, 1000.000000000000000 ) ;
#104378=DIRECTION ( 'NONE',  ( -0.7071067811865486830, -0.7071067811865464625, -0.000000000000000000 ) ) ;
#104379=VECTOR ( 'NONE', #100758, 1000.000000000000227 ) ;
#104380=DIRECTION ( 'NONE',  ( 0.7071067811865487940, -0.7071067811865463515, 0.000000000000000000 ) ) ;
#104381=ORIENTED_EDGE ( 'NONE', *, *, #111476, .T. ) ;
#104382=CARTESIAN_POINT ( 'NONE',  ( -11.99999999999991296, 20.96639925780204905, 5.000000000000000000 ) ) ;
#104383=FACE_BOUND ( 'NONE', #51131, .T. ) ;
#104384=ADVANCED_FACE ( 'NONE', ( #41215 ), #64404, .F. ) ;
#104385=ORIENTED_EDGE ( 'NONE', *, *, #89799, .T. ) ;
#104386=DIRECTION ( 'NONE',  ( 0.7071067811865486830, -0.7071067811865464625, -0.000000000000000000 ) ) ;
#104387=DIRECTION ( 'NONE',  ( 0.7071067811865487940, 0.7071067811865463515, 0.000000000000000000 ) ) ;
#104390=EDGE_CURVE ( 'NONE', #29472, #54913, #84729, .T. ) ;
#104391=ORIENTED_EDGE ( 'NONE', *, *, #107634, .F. ) ;
#104392=LINE ( 'NONE', #5051, #99076 ) ;
#104393=VERTEX_POINT ( 'NONE', #62283 ) ;
#104394=ORIENTED_EDGE ( 'NONE', *, *, #108893, .F. ) ;
#104397=VERTEX_POINT ( 'NONE', #9260 ) ;
#104398=VECTOR ( 'NONE', #68346, 1000.000000000000000 ) ;
#104399=EDGE_CURVE ( 'NONE', #109227, #129172, #86167, .T. ) ;
#104400=FACE_OUTER_BOUND ( 'NONE', #89003, .T. ) ;
#104403=EDGE_LOOP ( 'NONE', ( #120050, #80050, #114286, #42495 ) ) ;
#104405=EDGE_CURVE ( 'NONE', #77276, #110346, #140522, .T. ) ;
#104407=CARTESIAN_POINT ( 'NONE',  ( 2.999999999999978240, 2.342191155542454162, -5.001666872980091938 ) ) ;
#104408=FACE_OUTER_BOUND ( 'NONE', #58800, .T. ) ;
#104409=CARTESIAN_POINT ( 'NONE',  ( 14.99451991528749595, 28.92564299267948513, 4.000000000000000000 ) ) ;
#104410=DIRECTION ( 'NONE',  ( -0.7071067811865487940, 0.7071067811865463515, 0.000000000000000000 ) ) ;
#104411=DIRECTION ( 'NONE',  ( 0.6830127018922181881, 0.6830127018922202975, -0.2588190451025214056 ) ) ;
#104412=ORIENTED_EDGE ( 'NONE', *, *, #94025, .F. ) ;
#104413=ORIENTED_EDGE ( 'NONE', *, *, #52476, .F. ) ;
#104414=EDGE_CURVE ( 'NONE', #107388, #108114, #128252, .T. ) ;
#104415=ORIENTED_EDGE ( 'NONE', *, *, #8085, .T. ) ;
#104416=VECTOR ( 'NONE', #54213, 1000.000000000000000 ) ;
#104417=ORIENTED_EDGE ( 'NONE', *, *, #9233, .T. ) ;
#104419=ORIENTED_EDGE ( 'NONE', *, *, #28610, .T. ) ;
#104420=FACE_OUTER_BOUND ( 'NONE', #16614, .T. ) ;
#104421=DIRECTION ( 'NONE',  ( 0.7071067811865487940, 0.7071067811865463515, -0.000000000000000000 ) ) ;
#104422=ORIENTED_EDGE ( 'NONE', *, *, #26831, .T. ) ;
#104423=EDGE_CURVE ( 'NONE', #130424, #34219, #85420, .T. ) ;
#104424=DIRECTION ( 'NONE',  ( -0.7071067811865486830, -0.7071067811865464625, 0.000000000000000000 ) ) ;
#104426=ORIENTED_EDGE ( 'NONE', *, *, #131926, .F. ) ;
#104427=CARTESIAN_POINT ( 'NONE',  ( 33.48921356237309510, -27.52281430457078670, 5.000000000000000000 ) ) ;
#104428=EDGE_CURVE ( 'NONE', #135515, #96824, #137245, .T. ) ;
#104429=PLANE ( 'NONE',  #119082 ) ;
#104431=ORIENTED_EDGE ( 'NONE', *, *, #5839, .F. ) ;
#104433=CARTESIAN_POINT ( 'NONE',  ( 8.994519915287490619, 28.92564299267944250, 4.000000000000000000 ) ) ;
#104434=DIRECTION ( 'NONE',  ( 0.6830127018922180770, -0.6830127018922204085, -0.2588190451025213501 ) ) ;
#104435=DIRECTION ( 'NONE',  ( 0.7071067811865486830, -0.7071067811865464625, -0.000000000000000000 ) ) ;
#104436=VERTEX_POINT ( 'NONE', #20159 ) ;
#104437=EDGE_LOOP ( 'NONE', ( #128669, #112720, #35844, #14072 ) ) ;
#104438=PLANE ( 'NONE',  #72789 ) ;
#104439=ORIENTED_EDGE ( 'NONE', *, *, #7937, .T. ) ;
#104440=CARTESIAN_POINT ( 'NONE',  ( 42.48921356237308800, -27.52281430457085065, 5.000000000000000000 ) ) ;
#104441=LINE ( 'NONE', #105165, #136623 ) ;
#104442=PLANE ( 'NONE',  #70608 ) ;
#104444=LINE ( 'NONE', #24755, #46981 ) ;
#104446=ORIENTED_EDGE ( 'NONE', *, *, #104734, .F. ) ;
#104447=VECTOR ( 'NONE', #119208, 1000.000000000000000 ) ;
#104448=CARTESIAN_POINT ( 'NONE',  ( -28.64175702458843276, 15.75929247661555799, 19.34181609438706317 ) ) ;
#104449=VECTOR ( 'NONE', #12895, 1000.000000000000000 ) ;
#104450=DIRECTION ( 'NONE',  ( -0.000000000000000000, -1.000000000000000000, -0.000000000000000000 ) ) ;
#104452=VERTEX_POINT ( 'NONE', #107185 ) ;
#104453=DIRECTION ( 'NONE',  ( -0.000000000000000000, -0.3543493200069152693, 0.9351131265310292928 ) ) ;
#104454=VECTOR ( 'NONE', #15484, 1000.000000000000000 ) ;
#104456=LINE ( 'NONE', #91467, #130336 ) ;
#104457=VECTOR ( 'NONE', #97271, 1000.000000000000000 ) ;
#104458=VERTEX_POINT ( 'NONE', #7860 ) ;
#104459=CARTESIAN_POINT ( 'NONE',  ( 0.1839886062690032631, 28.73617430169787568, 5.000000000000000000 ) ) ;
#104461=ORIENTED_EDGE ( 'NONE', *, *, #134261, .T. ) ;
#104462=CARTESIAN_POINT ( 'NONE',  ( 21.18398860626899349, 28.73617430169802134, 5.000000000000000000 ) ) ;
#104463=VECTOR ( 'NONE', #141636, 1000.000000000000000 ) ;
#104467=DIRECTION ( 'NONE',  ( 0.7071067811865487940, 0.7071067811865463515, 0.000000000000000000 ) ) ;
#104469=ORIENTED_EDGE ( 'NONE', *, *, #1737, .F. ) ;
#104470=VECTOR ( 'NONE', #106489, 1000.000000000000000 ) ;
#104472=DIRECTION ( 'NONE',  ( 1.000000000000000000, 0.000000000000000000, 0.000000000000000000 ) ) ;
#104473=EDGE_CURVE ( 'NONE', #85340, #63769, #28218, .T. ) ;
#104474=DIRECTION ( 'NONE',  ( 0.7071067811865487940, 0.7071067811865463515, 0.000000000000000000 ) ) ;
#104475=DIRECTION ( 'NONE',  ( -0.6830127018922180770, -0.6830127018922202975, -0.2588190451025213501 ) ) ;
#104478=DIRECTION ( 'NONE',  ( 0.6830127018922180770, -0.6830127018922204085, -0.2588190451025213501 ) ) ;
#104480=CARTESIAN_POINT ( 'NONE',  ( -75.48921356237309510, -27.52281430457107803, 5.000000000000000000 ) ) ;
#104483=ORIENTED_EDGE ( 'NONE', *, *, #57122, .T. ) ;
#104484=ORIENTED_EDGE ( 'NONE', *, *, #105643, .T. ) ;
#104486=VECTOR ( 'NONE', #143412, 1000.000000000000000 ) ;
#104487=ORIENTED_EDGE ( 'NONE', *, *, #128187, .F. ) ;
#104488=ORIENTED_EDGE ( 'NONE', *, *, #135180, .F. ) ;
#104489=EDGE_CURVE ( 'NONE', #102767, #50434, #51405, .T. ) ;
#104490=AXIS2_PLACEMENT_3D ( 'NONE', #51670, #87142, #140784 ) ;
#104491=EDGE_LOOP ( 'NONE', ( #54599, #46239, #63454, #29840 ) ) ;
#104495=ORIENTED_EDGE ( 'NONE', *, *, #72936, .T. ) ;
#104496=CARTESIAN_POINT ( 'NONE',  ( -4.251544128675727841, -11.24070752338416845, 10.39518518046010342 ) ) ;
#104497=DIRECTION ( 'NONE',  ( -0.7071067811865486830, 0.7071067811865464625, 0.000000000000000000 ) ) ;
#104500=ADVANCED_FACE ( 'NONE', ( #17326 ), #19471, .T. ) ;
#104501=VECTOR ( 'NONE', #80611, 1000.000000000000000 ) ;
#104502=ORIENTED_EDGE ( 'NONE', *, *, #130310, .T. ) ;
#104503=DIRECTION ( 'NONE',  ( -0.000000000000000000, 0.3543493200069153248, 0.9351131265310292928 ) ) ;
#104504=DIRECTION ( 'NONE',  ( -0.6830127018922180770, -0.6830127018922204085, -0.2588190451025213501 ) ) ;
#104505=EDGE_CURVE ( 'NONE', #22185, #10056, #52099, .T. ) ;
#104506=LINE ( 'NONE', #135723, #35702 ) ;
#104507=CARTESIAN_POINT ( 'NONE',  ( -18.18398860626898994, 28.73617430169800002, 5.000000000000000000 ) ) ;
#104509=DIRECTION ( 'NONE',  ( 0.6830127018922181881, 0.6830127018922202975, -0.2588190451025214056 ) ) ;
#104510=ADVANCED_FACE ( 'NONE', ( #117330 ), #106440, .T. ) ;
#104514=EDGE_LOOP ( 'NONE', ( #6363, #123135, #44031, #115159 ) ) ;
#104515=ORIENTED_EDGE ( 'NONE', *, *, #32423, .T. ) ;
#104518=ORIENTED_EDGE ( 'NONE', *, *, #124575, .T. ) ;
#104519=ADVANCED_FACE ( 'NONE', ( #128943 ), #29614, .F. ) ;
#104520=CARTESIAN_POINT ( 'NONE',  ( -7.499999999999942268, -10.91253812416064406, 4.000000000000000000 ) ) ;
#104521=VECTOR ( 'NONE', #95793, 1000.000000000000000 ) ;
#104522=LINE ( 'NONE', #50870, #33980 ) ;
#104523=ORIENTED_EDGE ( 'NONE', *, *, #127989, .F. ) ;
#104524=AXIS2_PLACEMENT_3D ( 'NONE', #121932, #102370, #23339 ) ;
#104525=PLANE ( 'NONE',  #10915 ) ;
#104526=PLANE ( 'NONE',  #2830 ) ;
#104527=ADVANCED_FACE ( 'NONE', ( #118774 ), #107874, .F. ) ;
#104528=CARTESIAN_POINT ( 'NONE',  ( -42.29974487139158157, -27.71228299555235708, 4.000000000000000000 ) ) ;
#104530=ORIENTED_EDGE ( 'NONE', *, *, #53590, .F. ) ;
#104531=DIRECTION ( 'NONE',  ( -0.000000000000000000, -0.3543493200069152693, 0.9351131265310292928 ) ) ;
#104532=ORIENTED_EDGE ( 'NONE', *, *, #121780, .T. ) ;
#104533=AXIS2_PLACEMENT_3D ( 'NONE', #53675, #142118, #140649 ) ;
#104534=DIRECTION ( 'NONE',  ( 0.7071067811865487940, 0.7071067811865463515, 0.000000000000000000 ) ) ;
#104535=EDGE_CURVE ( 'NONE', #16006, #17089, #100616, .T. ) ;
#104536=CARTESIAN_POINT ( 'NONE',  ( -16.99806943317890173, -22.22500000000000142, 4.500000000000000888 ) ) ;
#104538=DIRECTION ( 'NONE',  ( 0.6830127018922181881, 0.6830127018922202975, -0.2588190451025214056 ) ) ;
#104542=PLANE ( 'NONE',  #17025 ) ;
#104543=CARTESIAN_POINT ( 'NONE',  ( -0.7071067811865398012, 11.25929247661561305, 5.000000000000000000 ) ) ;
#104545=EDGE_CURVE ( 'NONE', #16928, #6491, #142682, .T. ) ;
#104546=DIRECTION ( 'NONE',  ( 0.7071067811865486830, -0.7071067811865464625, -0.000000000000000000 ) ) ;
#104547=VECTOR ( 'NONE', #116287, 1000.000000000000000 ) ;
#104548=EDGE_CURVE ( 'NONE', #137243, #127621, #78152, .T. ) ;
#104553=CARTESIAN_POINT ( 'NONE',  ( -12.48921356237309155, -27.52281430457064104, 5.000000000000000000 ) ) ;
#104554=ORIENTED_EDGE ( 'NONE', *, *, #54596, .T. ) ;
#104556=FACE_OUTER_BOUND ( 'NONE', #112197, .T. ) ;
#104557=VECTOR ( 'NONE', #80944, 1000.000000000000000 ) ;
#104558=VECTOR ( 'NONE', #20439, 1000.000000000000000 ) ;
#104559=ORIENTED_EDGE ( 'NONE', *, *, #36333, .F. ) ;
#104560=EDGE_CURVE ( 'NONE', #128957, #70018, #99144, .T. ) ;
#104561=ADVANCED_FACE ( 'NONE', ( #78877 ), #133947, .F. ) ;
#104563=EDGE_LOOP ( 'NONE', ( #5432, #137959, #69203, #9355 ) ) ;
#104565=VECTOR ( 'NONE', #125894, 1000.000000000000000 ) ;
#104566=VECTOR ( 'NONE', #108201, 1000.000000000000000 ) ;
#104568=VECTOR ( 'NONE', #77313, 1000.000000000000000 ) ;
#104569=EDGE_CURVE ( 'NONE', #41530, #50028, #33936, .T. ) ;
#104570=VECTOR ( 'NONE', #138993, 1000.000000000000000 ) ;
#104571=CARTESIAN_POINT ( 'NONE',  ( 57.48921356237308800, -27.52281430457095368, 5.000000000000000000 ) ) ;
#104572=FACE_BOUND ( 'NONE', #30333, .T. ) ;
#104573=EDGE_CURVE ( 'NONE', #12969, #17742, #44097, .T. ) ;
#104580=VERTEX_POINT ( 'NONE', #120171 ) ;
#104581=CARTESIAN_POINT ( 'NONE',  ( 30.48921356237309510, -27.52281430457076894, 5.000000000000000000 ) ) ;
#104582=ORIENTED_EDGE ( 'NONE', *, *, #124857, .F. ) ;
#104585=ORIENTED_EDGE ( 'NONE', *, *, #141111, .T. ) ;
#104586=EDGE_CURVE ( 'NONE', #89926, #105060, #54975, .T. ) ;
#104587=PLANE ( 'NONE',  #132151 ) ;
#104588=FACE_OUTER_BOUND ( 'NONE', #19720, .T. ) ;
#104589=EDGE_LOOP ( 'NONE', ( #17671, #126573, #120812, #131825 ) ) ;
#104590=EDGE_CURVE ( 'NONE', #107568, #31251, #97747, .T. ) ;
#104592=VECTOR ( 'NONE', #89574, 1000.000000000000227 ) ;
#104593=LINE ( 'NONE', #5257, #40933 ) ;
#104594=CARTESIAN_POINT ( 'NONE',  ( 25.49999999999982592, -17.56887692260762535, 4.000000000000000000 ) ) ;
#104595=LINE ( 'NONE', #40094, #110657 ) ;
#104597=CARTESIAN_POINT ( 'NONE',  ( 31.49999999999979039, -17.94781430457064531, 5.000000000000000000 ) ) ;
#104599=EDGE_LOOP ( 'NONE', ( #17885, #35274, #110000, #128321 ) ) ;
#104600=VECTOR ( 'NONE', #140027, 1000.000000000000227 ) ;
#104601=FACE_OUTER_BOUND ( 'NONE', #140113, .T. ) ;
#104602=CARTESIAN_POINT ( 'NONE',  ( 26.99999999999981526, 20.96639925780204905, 5.000000000000000000 ) ) ;
#104603=ORIENTED_EDGE ( 'NONE', *, *, #116514, .T. ) ;
#104604=VERTEX_POINT ( 'NONE', #133257 ) ;
#104607=LINE ( 'NONE', #4512, #122562 ) ;
#104609=PLANE ( 'NONE',  #138916 ) ;
#104611=ADVANCED_FACE ( 'NONE', ( #88316 ), #123085, .F. ) ;
#104612=CARTESIAN_POINT ( 'NONE',  ( 2.510786437626908008, -27.52281430457053446, 5.000000000000000000 ) ) ;
#104614=PLANE ( 'NONE',  #135213 ) ;
#104615=ORIENTED_EDGE ( 'NONE', *, *, #124511, .F. ) ;
#104616=CARTESIAN_POINT ( 'NONE',  ( 6.516654386410396071, 22.22500000000000142, 4.500000000000000888 ) ) ;
#104617=DIRECTION ( 'NONE',  ( 0.7071067811865487940, 0.7071067811865463515, 0.000000000000000000 ) ) ;
#104620=LINE ( 'NONE', #138702, #105095 ) ;
#104621=EDGE_LOOP ( 'NONE', ( #15350, #131333, #57056, #33813 ) ) ;
#104625=DIRECTION ( 'NONE',  ( -0.000000000000000000, 0.3543493200069153248, 0.9351131265310292928 ) ) ;
#104626=CARTESIAN_POINT ( 'NONE',  ( -3.299744871391591339, -27.71228299555208352, 4.000000000000000000 ) ) ;
#104628=ORIENTED_EDGE ( 'NONE', *, *, #85426, .T. ) ;
#104629=LINE ( 'NONE', #114768, #47258 ) ;
#104631=DIRECTION ( 'NONE',  ( -0.6830127018922181881, 0.6830127018922202975, -0.2588190451025214056 ) ) ;
#104632=EDGE_LOOP ( 'NONE', ( #21811, #132023, #13401, #63312 ) ) ;
#104633=LINE ( 'NONE', #93767, #9124 ) ;
#104637=DIRECTION ( 'NONE',  ( -0.3543493200069162685, -0.000000000000000000, -0.9351131265310288487 ) ) ;
#104638=LINE ( 'NONE', #26383, #57695 ) ;
#104640=VERTEX_POINT ( 'NONE', #32506 ) ;
#104641=VECTOR ( 'NONE', #122484, 1000.000000000000000 ) ;
#104644=CARTESIAN_POINT ( 'NONE',  ( -51.18398860626899705, 28.73617430169823095, 5.000000000000000000 ) ) ;
#104645=CARTESIAN_POINT ( 'NONE',  ( 0.000000000000000000, 0.000000000000000000, 5.000000000000000000 ) ) ;
#104646=LINE ( 'NONE', #5319, #113159 ) ;
#104647=LINE ( 'NONE', #69189, #51380 ) ;
#104648=VERTEX_POINT ( 'NONE', #65147 ) ;
#104649=DIRECTION ( 'NONE',  ( 0.3543493200069162685, -0.000000000000000000, -0.9351131265310288487 ) ) ;
#104650=CARTESIAN_POINT ( 'NONE',  ( -75.48921356237309510, -27.52281430457107803, 5.000000000000000000 ) ) ;
#104652=AXIS2_PLACEMENT_3D ( 'NONE', #74698, #118879, #11516 ) ;
#104656=VECTOR ( 'NONE', #99406, 1000.000000000000000 ) ;
#104658=VERTEX_POINT ( 'NONE', #66559 ) ;
#104659=FACE_OUTER_BOUND ( 'NONE', #83375, .T. ) ;
#104660=ORIENTED_EDGE ( 'NONE', *, *, #123139, .F. ) ;
#104661=EDGE_CURVE ( 'NONE', #93122, #3321, #23003, .T. ) ;
#104662=ORIENTED_EDGE ( 'NONE', *, *, #48932, .F. ) ;
#104663=AXIS2_PLACEMENT_3D ( 'NONE', #33596, #76365, #30732 ) ;
#104664=VECTOR ( 'NONE', #10670, 1000.000000000000000 ) ;
#104665=CARTESIAN_POINT ( 'NONE',  ( -36.18398860626899705, 28.73617430169812437, 5.000000000000000000 ) ) ;
#104667=FACE_OUTER_BOUND ( 'NONE', #66973, .T. ) ;
#104669=LINE ( 'NONE', #103930, #106352 ) ;
#104670=CARTESIAN_POINT ( 'NONE',  ( -34.92500000000001137, -16.19990548397262842, 4.759050581649339584 ) ) ;
#104672=ADVANCED_FACE ( 'NONE', ( #98458 ), #43376, .F. ) ;
#104673=ADVANCED_FACE ( 'NONE', ( #557 ), #11411, .F. ) ;
#104674=ORIENTED_EDGE ( 'NONE', *, *, #91289, .F. ) ;
#104675=CARTESIAN_POINT ( 'NONE',  ( 75.48921356237309510, -27.52281430457107803, 5.000000000000000000 ) ) ;
#104676=LINE ( 'NONE', #5343, #83914 ) ;
#104677=DIRECTION ( 'NONE',  ( -0.000000000000000000, 0.000000000000000000, 1.000000000000000000 ) ) ;
#104678=CARTESIAN_POINT ( 'NONE',  ( -27.70710678118635073, 11.25929247661560595, 5.000000000000000000 ) ) ;
#104679=CARTESIAN_POINT ( 'NONE',  ( -0.2997448713915885632, -27.71228299555206220, 4.000000000000000000 ) ) ;
#104682=ADVANCED_FACE ( 'NONE', ( #70854 ), #46261, .T. ) ;
#104683=FACE_OUTER_BOUND ( 'NONE', #31521, .T. ) ;
#104684=VERTEX_POINT ( 'NONE', #102035 ) ;
#104685=EDGE_LOOP ( 'NONE', ( #114418, #39179, #92625, #92948 ) ) ;
#104687=DIRECTION ( 'NONE',  ( -0.6830127018922180770, -0.6830127018922204085, -0.2588190451025213501 ) ) ;
#104688=EDGE_CURVE ( 'NONE', #66020, #76576, #23316, .T. ) ;
#104689=CARTESIAN_POINT ( 'NONE',  ( 45.18398860626900415, 28.73617430169818832, 5.000000000000000000 ) ) ;
#104690=DIRECTION ( 'NONE',  ( 0.7071067811865486830, -0.7071067811865464625, -0.000000000000000000 ) ) ;
#104691=ORIENTED_EDGE ( 'NONE', *, *, #70704, .T. ) ;
#104693=PLANE ( 'NONE',  #53779 ) ;
#104696=DIRECTION ( 'NONE',  ( -0.7071067811865487940, 0.7071067811865463515, -0.000000000000000000 ) ) ;
#104698=AXIS2_PLACEMENT_3D ( 'NONE', #34739, #21710, #78978 ) ;
#104699=DIRECTION ( 'NONE',  ( 0.7071067811865486830, -0.7071067811865464625, -0.000000000000000000 ) ) ;
#104700=VERTEX_POINT ( 'NONE', #126614 ) ;
#104701=ORIENTED_EDGE ( 'NONE', *, *, #63023, .T. ) ;
#104702=VECTOR ( 'NONE', #122334, 1000.000000000000227 ) ;
#104703=DIRECTION ( 'NONE',  ( 1.000000000000000000, 0.000000000000000000, 0.000000000000000000 ) ) ;
#104704=DIRECTION ( 'NONE',  ( -0.7071067811865487940, 0.7071067811865463515, -0.000000000000000000 ) ) ;
#104705=FACE_OUTER_BOUND ( 'NONE', #59433, .T. ) ;
#104706=DIRECTION ( 'NONE',  ( 0.7071067811865487940, 0.7071067811865463515, -0.000000000000000000 ) ) ;
#104707=LINE ( 'NONE', #5374, #60451 ) ;
#104708=CARTESIAN_POINT ( 'NONE',  ( 4.589909354801656072, 9.759292476615625489, 11.28811694763779627 ) ) ;
#104709=ORIENTED_EDGE ( 'NONE', *, *, #12234, .F. ) ;
#104710=CARTESIAN_POINT ( 'NONE',  ( 1.499999999999987566, -8.568876922607726598, 4.000000000000000000 ) ) ;
#104711=DIRECTION ( 'NONE',  ( 0.6830127018922181881, 0.6830127018922202975, -0.2588190451025214056 ) ) ;
#104712=FACE_OUTER_BOUND ( 'NONE', #68782, .T. ) ;
#104715=LINE ( 'NONE', #17003, #64634 ) ;
#104717=ORIENTED_EDGE ( 'NONE', *, *, #22672, .F. ) ;
#104718=CARTESIAN_POINT ( 'NONE',  ( -39.18398860626899705, 28.73617430169814568, 5.000000000000000000 ) ) ;
#104720=VECTOR ( 'NONE', #25739, 1000.000000000000000 ) ;
#104721=EDGE_CURVE ( 'NONE', #59049, #45425, #37509, .T. ) ;
#104723=CARTESIAN_POINT ( 'NONE',  ( -25.49999999999982592, -20.56887692260760048, 4.000000000000000000 ) ) ;
#104724=ORIENTED_EDGE ( 'NONE', *, *, #27255, .T. ) ;
#104725=EDGE_LOOP ( 'NONE', ( #88757, #47247, #78973, #81510 ) ) ;
#104726=VECTOR ( 'NONE', #92005, 1000.000000000000000 ) ;
#104728=CARTESIAN_POINT ( 'NONE',  ( -17.99999999999986855, -4.447814304570788302, 5.000000000000000000 ) ) ;
#104730=EDGE_CURVE ( 'NONE', #32716, #49377, #57138, .T. ) ;
#104731=ORIENTED_EDGE ( 'NONE', *, *, #98539, .F. ) ;
#104732=LINE ( 'NONE', #51086, #81449 ) ;
#104733=VERTEX_POINT ( 'NONE', #15683 ) ;
#104734=EDGE_CURVE ( 'NONE', #99443, #109446, #58589, .T. ) ;
#104735=CARTESIAN_POINT ( 'NONE',  ( -11.70025512860841133, -27.71228299555198049, 4.000000000000000000 ) ) ;
#104736=DIRECTION ( 'NONE',  ( 1.000000000000000000, 0.000000000000000000, 0.000000000000000000 ) ) ;
#104737=AXIS2_PLACEMENT_3D ( 'NONE', #59562, #93598, #58885 ) ;
#104739=EDGE_CURVE ( 'NONE', #9218, #81079, #4800, .T. ) ;
#104740=FACE_BOUND ( 'NONE', #123957, .T. ) ;
#104742=DIRECTION ( 'NONE',  ( -0.000000000000000000, -0.3543493200069153248, -0.9351131265310291818 ) ) ;
#104743=PLANE ( 'NONE',  #122363 ) ;
#104744=VECTOR ( 'NONE', #136421, 999.9999999999998863 ) ;
#104745=DIRECTION ( 'NONE',  ( 0.6830127018922180770, -0.6830127018922204085, -0.2588190451025213501 ) ) ;
#104747=EDGE_CURVE ( 'NONE', #95610, #39863, #3405, .T. ) ;
#104748=PLANE ( 'NONE',  #2350 ) ;
#104750=EDGE_LOOP ( 'NONE', ( #55175, #58657, #34475, #135075 ) ) ;
#104751=ORIENTED_EDGE ( 'NONE', *, *, #110326, .F. ) ;
#104753=ORIENTED_EDGE ( 'NONE', *, *, #40546, .T. ) ;
#104754=EDGE_CURVE ( 'NONE', #136233, #49064, #36083, .T. ) ;
#104756=CARTESIAN_POINT ( 'NONE',  ( -11.81601139373100651, 28.73617430169779041, 5.000000000000000000 ) ) ;
#104757=VECTOR ( 'NONE', #90024, 1000.000000000000000 ) ;
#104758=AXIS2_PLACEMENT_3D ( 'NONE', #13662, #70274, #123193 ) ;
#104759=VECTOR ( 'NONE', #78545, 1000.000000000000000 ) ;
#104760=VECTOR ( 'NONE', #16152, 1000.000000000000227 ) ;
#104761=VECTOR ( 'NONE', #63075, 1000.000000000000000 ) ;
#104762=DIRECTION ( 'NONE',  ( 0.6830127018922180770, -0.6830127018922204085, -0.2588190451025213501 ) ) ;
#104763=ORIENTED_EDGE ( 'NONE', *, *, #33892, .T. ) ;
#104764=PLANE ( 'NONE',  #29844 ) ;
#104766=DIRECTION ( 'NONE',  ( -0.6830127018922181881, 0.6830127018922202975, -0.2588190451025214056 ) ) ;
#104767=CARTESIAN_POINT ( 'NONE',  ( -2.999999999999975131, 14.96639925780211122, 5.000000000000000000 ) ) ;
#104768=PLANE ( 'NONE',  #125690 ) ;
#104770=AXIS2_PLACEMENT_3D ( 'NONE', #84920, #129134, #142181 ) ;
#104771=CARTESIAN_POINT ( 'NONE',  ( -3.706123077391934917, 22.22500000000000142, 4.000000000000000000 ) ) ;
#104772=EDGE_LOOP ( 'NONE', ( #109302, #21757, #135025, #128953 ) ) ;
#104773=PLANE ( 'NONE',  #114398 ) ;
#104774=DIRECTION ( 'NONE',  ( -0.7071067811865487940, 0.7071067811865463515, -0.000000000000000000 ) ) ;
#104776=EDGE_CURVE ( 'NONE', #9288, #48047, #90444, .T. ) ;
#104777=EDGE_LOOP ( 'NONE', ( #113947, #45991, #99282, #135901 ) ) ;
#104778=ORIENTED_EDGE ( 'NONE', *, *, #67790, .F. ) ;
#104780=ORIENTED_EDGE ( 'NONE', *, *, #128969, .F. ) ;
#104781=EDGE_CURVE ( 'NONE', #7366, #120044, #4079, .T. ) ;
#104782=VECTOR ( 'NONE', #67047, 999.9999999999998863 ) ;
#104785=ORIENTED_EDGE ( 'NONE', *, *, #143166, .T. ) ;
#104786=DIRECTION ( 'NONE',  ( -0.7071067811865486830, 0.7071067811865464625, 0.000000000000000000 ) ) ;
#104787=ORIENTED_EDGE ( 'NONE', *, *, #15419, .T. ) ;
#104788=CYLINDRICAL_SURFACE ( 'NONE', #81218, 0.5000000000000004441 ) ;
#104790=DIRECTION ( 'NONE',  ( 0.000000000000000000, 1.000000000000000000, 0.000000000000000000 ) ) ;
#104791=ORIENTED_EDGE ( 'NONE', *, *, #123913, .F. ) ;
#104793=ADVANCED_FACE ( 'NONE', ( #134688 ), #124495, .F. ) ;
#104795=LINE ( 'NONE', #119741, #106346 ) ;
#104796=ORIENTED_EDGE ( 'NONE', *, *, #47082, .T. ) ;
#104798=DIRECTION ( 'NONE',  ( 0.7071067811865487940, -0.7071067811865463515, 0.000000000000000000 ) ) ;
#104799=ORIENTED_EDGE ( 'NONE', *, *, #61687, .T. ) ;
#104801=ORIENTED_EDGE ( 'NONE', *, *, #65513, .T. ) ;
#104802=AXIS2_PLACEMENT_3D ( 'NONE', #9183, #53454, #96915 ) ;
#104804=ORIENTED_EDGE ( 'NONE', *, *, #100168, .F. ) ;
#104805=LINE ( 'NONE', #59886, #128242 ) ;
#104806=VECTOR ( 'NONE', #143045, 1000.000000000000227 ) ;
#104807=DIRECTION ( 'NONE',  ( -0.7071067811865486830, -0.7071067811865464625, -0.000000000000000000 ) ) ;
#104808=CARTESIAN_POINT ( 'NONE',  ( -22.99806943317885555, -22.22500000000000142, 4.500000000000000888 ) ) ;
#104809=LINE ( 'NONE', #15609, #113108 ) ;
#104810=EDGE_CURVE ( 'NONE', #71320, #65251, #136797, .T. ) ;
#104811=DIRECTION ( 'NONE',  ( 0.3543493200069162685, -0.000000000000000000, -0.9351131265310288487 ) ) ;
#104812=VERTEX_POINT ( 'NONE', #13565 ) ;
#104813=CARTESIAN_POINT ( 'NONE',  ( -26.99999999999980815, 18.08204922493370503, 0.9627537363045496344 ) ) ;
#104814=CARTESIAN_POINT ( 'NONE',  ( -21.32816939922337696, -15.74070752338412049, 4.000000000000000000 ) ) ;
#104816=FACE_OUTER_BOUND ( 'NONE', #111007, .T. ) ;
#104818=VERTEX_POINT ( 'NONE', #135403 ) ;
#104819=ORIENTED_EDGE ( 'NONE', *, *, #118057, .F. ) ;
#104820=VECTOR ( 'NONE', #35052, 1000.000000000000000 ) ;
#104822=CARTESIAN_POINT ( 'NONE',  ( 8.999999999999944933, -16.44781430457065952, 5.000000000000000000 ) ) ;
#104824=PLANE ( 'NONE',  #110132 ) ;
#104825=VECTOR ( 'NONE', #98965, 1000.000000000000000 ) ;
#104828=PLANE ( 'NONE',  #102028 ) ;
#104830=CARTESIAN_POINT ( 'NONE',  ( -18.18398860626898994, 28.73617430169800002, 5.000000000000000000 ) ) ;
#104831=CARTESIAN_POINT ( 'NONE',  ( -3.489213562373097322, -27.52281430457057709, 5.000000000000000000 ) ) ;
#104832=DIRECTION ( 'NONE',  ( -0.6830127018922180770, -0.6830127018922204085, -0.2588190451025213501 ) ) ;
#104834=ORIENTED_EDGE ( 'NONE', *, *, #11226, .F. ) ;
#104835=EDGE_CURVE ( 'NONE', #33991, #51470, #115006, .T. ) ;
#104836=VECTOR ( 'NONE', #11272, 1000.000000000000000 ) ;
#104837=CARTESIAN_POINT ( 'NONE',  ( -25.49999999999982947, 5.696342897626483825, -7.587980461218456263 ) ) ;
#104838=ORIENTED_EDGE ( 'NONE', *, *, #75575, .F. ) ;
#104840=LINE ( 'NONE', #59933, #36722 ) ;
#104841=DIRECTION ( 'NONE',  ( 0.7071067811865486830, -0.7071067811865464625, -0.000000000000000000 ) ) ;
#104843=DIRECTION ( 'NONE',  ( 0.3543493200069162685, -0.000000000000000000, -0.9351131265310288487 ) ) ;
#104845=EDGE_CURVE ( 'NONE', #119845, #95357, #83141, .T. ) ;
#104848=VERTEX_POINT ( 'NONE', #30171 ) ;
#104850=DIRECTION ( 'NONE',  ( 0.7071067811865486830, -0.7071067811865464625, -0.000000000000000000 ) ) ;
#104851=ADVANCED_FACE ( 'NONE', ( #60714 ), #75147, .F. ) ;
#104853=EDGE_CURVE ( 'NONE', #76593, #103400, #51949, .T. ) ;
#104855=VERTEX_POINT ( 'NONE', #17843 ) ;
#104856=ADVANCED_FACE ( 'NONE', ( #127344 ), #62835, .F. ) ;
#104859=PLANE ( 'NONE',  #43783 ) ;
#104861=LINE ( 'NONE', #48346, #139459 ) ;
#104862=VECTOR ( 'NONE', #112661, 1000.000000000000000 ) ;
#104863=DIRECTION ( 'NONE',  ( 1.000000000000000000, -0.000000000000000000, 0.000000000000000000 ) ) ;
#104864=EDGE_CURVE ( 'NONE', #26671, #34581, #41777, .T. ) ;
#104865=ORIENTED_EDGE ( 'NONE', *, *, #109382, .T. ) ;
#104867=AXIS2_PLACEMENT_3D ( 'NONE', #3132, #80038, #45964 ) ;
#104869=EDGE_CURVE ( 'NONE', #70774, #64350, #107015, .T. ) ;
#104870=ORIENTED_EDGE ( 'NONE', *, *, #97667, .F. ) ;
#104872=DIRECTION ( 'NONE',  ( -0.7071067811865487940, 0.7071067811865463515, 0.000000000000000000 ) ) ;
#104874=DIRECTION ( 'NONE',  ( -0.6830127018922181881, 0.6830127018922202975, -0.2588190451025214056 ) ) ;
#104875=CARTESIAN_POINT ( 'NONE',  ( 0.000000000000000000, 0.000000000000000000, 5.000000000000000000 ) ) ;
#104876=EDGE_LOOP ( 'NONE', ( #9271, #131175, #116517, #109671 ) ) ;
#104877=LINE ( 'NONE', #26606, #58224 ) ;
#104879=DIRECTION ( 'NONE',  ( 0.7071067811865486830, -0.7071067811865464625, -0.000000000000000000 ) ) ;
#104882=EDGE_LOOP ( 'NONE', ( #119836, #125459, #20160, #62758 ) ) ;
#104883=CARTESIAN_POINT ( 'NONE',  ( 29.84387692260737523, -22.22500000000000142, 4.000000000000000000 ) ) ;
#104884=DIRECTION ( 'NONE',  ( -0.3543493200069162685, -0.000000000000000000, -0.9351131265310288487 ) ) ;
#104886=ADVANCED_FACE ( 'NONE', ( #105572 ), #49824, .F. ) ;
#104888=VERTEX_POINT ( 'NONE', #93994 ) ;
#104889=EDGE_LOOP ( 'NONE', ( #83826, #117443, #78621, #87156 ) ) ;
#104893=ORIENTED_EDGE ( 'NONE', *, *, #61608, .T. ) ;
#104894=DIRECTION ( 'NONE',  ( 0.6830127018922181881, 0.6830127018922202975, -0.2588190451025214056 ) ) ;
#104895=LINE ( 'NONE', #3419, #119717 ) ;
#104896=CARTESIAN_POINT ( 'NONE',  ( -42.29974487139158157, -27.71228299555235708, 4.000000000000000000 ) ) ;
#104898=EDGE_LOOP ( 'NONE', ( #71128, #108109, #78952, #72756 ) ) ;
#104899=LINE ( 'NONE', #140384, #44543 ) ;
#104900=DIRECTION ( 'NONE',  ( 0.000000000000000000, 0.000000000000000000, 1.000000000000000000 ) ) ;
#104901=VECTOR ( 'NONE', #88402, 1000.000000000000000 ) ;
#104902=ORIENTED_EDGE ( 'NONE', *, *, #123570, .T. ) ;
#104904=CARTESIAN_POINT ( 'NONE',  ( -24.84463820744543838, 1.742823668393624903, 4.000000000000000000 ) ) ;
#104905=EDGE_CURVE ( 'NONE', #100977, #99513, #39658, .T. ) ;
#104907=LINE ( 'NONE', #128797, #107104 ) ;
#104908=EDGE_CURVE ( 'NONE', #97859, #124430, #43664, .T. ) ;
#104910=VECTOR ( 'NONE', #99628, 999.9999999999998863 ) ;
#104911=EDGE_LOOP ( 'NONE', ( #2505, #119551, #23004, #74493 ) ) ;
#104912=FACE_OUTER_BOUND ( 'NONE', #27520, .T. ) ;
#104913=LINE ( 'NONE', #62868, #3742 ) ;
#104915=LINE ( 'NONE', #28803, #67448 ) ;
#104916=DIRECTION ( 'NONE',  ( -0.3543493200069162685, -0.000000000000000000, -0.9351131265310288487 ) ) ;
#104917=ADVANCED_FACE ( 'NONE', ( #29450 ), #62112, .F. ) ;
#104918=VECTOR ( 'NONE', #24594, 1000.000000000000227 ) ;
#104919=CARTESIAN_POINT ( 'NONE',  ( -11.67183060077638679, -15.74070752338412049, 4.000000000000000000 ) ) ;
#104920=ORIENTED_EDGE ( 'NONE', *, *, #87587, .F. ) ;
#104921=ORIENTED_EDGE ( 'NONE', *, *, #100455, .F. ) ;
#104922=ORIENTED_EDGE ( 'NONE', *, *, #46556, .T. ) ;
#104923=EDGE_CURVE ( 'NONE', #57507, #102158, #96130, .T. ) ;
#104924=ORIENTED_EDGE ( 'NONE', *, *, #110139, .F. ) ;
#104925=VECTOR ( 'NONE', #64053, 1000.000000000000000 ) ;
#104926=DIRECTION ( 'NONE',  ( -0.6830127018922181881, 0.6830127018922202975, -0.2588190451025214056 ) ) ;
#104928=ORIENTED_EDGE ( 'NONE', *, *, #102968, .T. ) ;
#104929=CARTESIAN_POINT ( 'NONE',  ( 81.48921356237309510, -27.52281430457112066, 5.000000000000000000 ) ) ;
#104931=CARTESIAN_POINT ( 'NONE',  ( 51.18398860626899705, 28.73617430169823095, 5.000000000000000000 ) ) ;
#104932=CARTESIAN_POINT ( 'NONE',  ( -29.99999999999979750, -2.904428200921339354, -6.989807076074876946 ) ) ;
#104934=CARTESIAN_POINT ( 'NONE',  ( 3.183988606268992161, 28.73617430169789699, 5.000000000000000000 ) ) ;
#104935=ORIENTED_EDGE ( 'NONE', *, *, #80719, .T. ) ;
#104936=DIRECTION ( 'NONE',  ( -0.000000000000000000, 0.000000000000000000, 1.000000000000000000 ) ) ;
#104937=CARTESIAN_POINT ( 'NONE',  ( -19.62719212111867151, -2.766370489448051195, 4.185522593092492194 ) ) ;
#104938=EDGE_LOOP ( 'NONE', ( #110776, #110557, #59645, #75303, #105249 ) ) ;
#104939=LINE ( 'NONE', #125277, #133879 ) ;
#104940=EDGE_CURVE ( 'NONE', #85226, #98208, #61462, .T. ) ;
#104941=ORIENTED_EDGE ( 'NONE', *, *, #134713, .F. ) ;
#104942=ORIENTED_EDGE ( 'NONE', *, *, #5244, .T. ) ;
#104943=EDGE_CURVE ( 'NONE', #135502, #81560, #128774, .T. ) ;
#104944=VERTEX_POINT ( 'NONE', #8383 ) ;
#104945=ORIENTED_EDGE ( 'NONE', *, *, #121863, .F. ) ;
#104947=ORIENTED_EDGE ( 'NONE', *, *, #88335, .F. ) ;
#104948=CARTESIAN_POINT ( 'NONE',  ( 50.99451991528749062, 28.92564299267973738, 4.000000000000000000 ) ) ;
#104949=LINE ( 'NONE', #30245, #26480 ) ;
#104951=DIRECTION ( 'NONE',  ( -0.7071067811865486830, -0.7071067811865464625, 0.000000000000000000 ) ) ;
#104952=DIRECTION ( 'NONE',  ( -0.7071067811865487940, 0.7071067811865463515, -0.000000000000000000 ) ) ;
#104953=AXIS2_PLACEMENT_3D ( 'NONE', #108002, #121747, #684 ) ;
#104954=DIRECTION ( 'NONE',  ( -0.000000000000000000, 0.000000000000000000, 1.000000000000000000 ) ) ;
#104955=FACE_OUTER_BOUND ( 'NONE', #10725, .T. ) ;
#104956=VECTOR ( 'NONE', #24718, 1000.000000000000000 ) ;
#104957=ADVANCED_FACE ( 'NONE', ( #117859 ), #54805, .F. ) ;
#104960=ADVANCED_FACE ( 'NONE', ( #56267 ), #22137, .F. ) ;
#104962=ORIENTED_EDGE ( 'NONE', *, *, #21911, .F. ) ;
#104964=AXIS2_PLACEMENT_3D ( 'NONE', #132027, #18965, #54476 ) ;
#104966=DIRECTION ( 'NONE',  ( 0.7071067811865487940, 0.7071067811865463515, 0.000000000000000000 ) ) ;
#104967=EDGE_LOOP ( 'NONE', ( #122250, #134760, #118595, #68760 ) ) ;
#104968=FACE_OUTER_BOUND ( 'NONE', #29856, .T. ) ;
#104969=DIRECTION ( 'NONE',  ( 0.7071067811865486830, -0.7071067811865464625, -0.000000000000000000 ) ) ;
#104970=DIRECTION ( 'NONE',  ( -0.7071067811865486830, -0.7071067811865464625, 0.000000000000000000 ) ) ;
#104971=EDGE_CURVE ( 'NONE', #107217, #86260, #123298, .T. ) ;
#104974=ORIENTED_EDGE ( 'NONE', *, *, #20260, .T. ) ;
#104976=ORIENTED_EDGE ( 'NONE', *, *, #50246, .T. ) ;
#104977=VECTOR ( 'NONE', #22532, 1000.000000000000000 ) ;
#104978=VECTOR ( 'NONE', #100753, 1000.000000000000227 ) ;
#104980=DIRECTION ( 'NONE',  ( 0.7071067811865487940, 0.7071067811865463515, 0.000000000000000000 ) ) ;
#104981=DIRECTION ( 'NONE',  ( 1.000000000000000000, 0.000000000000000000, 0.000000000000000000 ) ) ;
#104982=DIRECTION ( 'NONE',  ( 0.6830127018922180770, -0.6830127018922204085, -0.2588190451025213501 ) ) ;
#104984=ORIENTED_EDGE ( 'NONE', *, *, #79328, .F. ) ;
#104985=VERTEX_POINT ( 'NONE', #98303 ) ;
#104986=LINE ( 'NONE', #94801, #72814 ) ;
#104987=LINE ( 'NONE', #70963, #83483 ) ;
#104988=CARTESIAN_POINT ( 'NONE',  ( -8.292986735706895374, -21.74070752338406010, 4.999753212805224223 ) ) ;
#104989=CARTESIAN_POINT ( 'NONE',  ( -15.70710678118643422, 11.25929247661561128, 5.000000000000000000 ) ) ;
#104990=AXIS2_PLACEMENT_3D ( 'NONE', #116385, #17078, #83792 ) ;
#104991=LINE ( 'NONE', #124613, #131923 ) ;
#104992=PLANE ( 'NONE',  #64280 ) ;
#104993=LINE ( 'NONE', #94109, #71735 ) ;
#104994=AXIS2_PLACEMENT_3D ( 'NONE', #97474, #64881, #54722 ) ;
#104995=CARTESIAN_POINT ( 'NONE',  ( -18.29974487139159223, -27.71228299555219010, 4.000000000000000000 ) ) ;
#104996=DIRECTION ( 'NONE',  ( 0.7071067811865486830, -0.7071067811865464625, -0.000000000000000000 ) ) ;
#104997=ORIENTED_EDGE ( 'NONE', *, *, #142417, .F. ) ;
#104999=DIRECTION ( 'NONE',  ( -0.000000000000000000, 0.3543493200069152138, -0.9351131265310292928 ) ) ;
#105000=ORIENTED_EDGE ( 'NONE', *, *, #28848, .T. ) ;
#105001=VECTOR ( 'NONE', #127847, 1000.000000000000000 ) ;
#105002=DIRECTION ( 'NONE',  ( 0.6830127018922181881, 0.6830127018922202975, -0.2588190451025214056 ) ) ;
#105004=ORIENTED_EDGE ( 'NONE', *, *, #45777, .F. ) ;
#105006=DIRECTION ( 'NONE',  ( -0.7071067811865486830, -0.7071067811865464625, 0.000000000000000000 ) ) ;
#105008=CARTESIAN_POINT ( 'NONE',  ( 34.92499999999998295, 4.444556126563224296, 11.73767485154041523 ) ) ;
#105009=VERTEX_POINT ( 'NONE', #131648 ) ;
#105010=VECTOR ( 'NONE', #3963, 1000.000000000000227 ) ;
#105011=CARTESIAN_POINT ( 'NONE',  ( -30.48921356237309510, -27.52281430457076894, 5.000000000000000000 ) ) ;
#105014=EDGE_CURVE ( 'NONE', #47828, #81835, #110565, .T. ) ;
#105015=DIRECTION ( 'NONE',  ( -0.7071067811865487940, 0.7071067811865463515, 0.000000000000000000 ) ) ;
#105016=VECTOR ( 'NONE', #17411, 1000.000000000000227 ) ;
#105017=CARTESIAN_POINT ( 'NONE',  ( 51.48921356237309510, -27.52281430457091460, 5.000000000000000000 ) ) ;
#105018=EDGE_CURVE ( 'NONE', #8091, #83438, #19523, .T. ) ;
#105019=EDGE_CURVE ( 'NONE', #10533, #51668, #55518, .T. ) ;
#105020=DIRECTION ( 'NONE',  ( -0.7071067811865487940, 0.7071067811865463515, 0.000000000000000000 ) ) ;
#105022=EDGE_CURVE ( 'NONE', #5639, #30178, #64974, .T. ) ;
#105026=VECTOR ( 'NONE', #25169, 1000.000000000000000 ) ;
#105027=CARTESIAN_POINT ( 'NONE',  ( -31.82816939922330235, 3.759292476615678336, 4.000000000000000000 ) ) ;
#105028=LINE ( 'NONE', #28197, #102251 ) ;
#105030=ADVANCED_FACE ( 'NONE', ( #133781 ), #87429, .T. ) ;
#105033=VERTEX_POINT ( 'NONE', #88868 ) ;
#105036=ORIENTED_EDGE ( 'NONE', *, *, #80690, .T. ) ;
#105038=EDGE_CURVE ( 'NONE', #97236, #6765, #132388, .T. ) ;
#105040=DIRECTION ( 'NONE',  ( 0.7071067811865487940, 0.7071067811865463515, 0.000000000000000000 ) ) ;
#105042=LINE ( 'NONE', #61578, #94038 ) ;
#105044=CARTESIAN_POINT ( 'NONE',  ( -18.29974487139159223, -27.71228299555219010, 4.000000000000000000 ) ) ;
#105045=FACE_OUTER_BOUND ( 'NONE', #44659, .T. ) ;
#105047=CARTESIAN_POINT ( 'NONE',  ( 1.499999999999996225, -4.533600742197694267, 5.000000000000000000 ) ) ;
#105049=EDGE_CURVE ( 'NONE', #46912, #43233, #98988, .T. ) ;
#105050=CARTESIAN_POINT ( 'NONE',  ( 0.000000000000000000, 0.000000000000000000, 5.000000000000000000 ) ) ;
#105051=DIRECTION ( 'NONE',  ( 1.000000000000000000, 0.000000000000000000, 0.000000000000000000 ) ) ;
#105054=DIRECTION ( 'NONE',  ( -0.7071067811865486830, -0.7071067811865464625, -0.000000000000000000 ) ) ;
#105055=CARTESIAN_POINT ( 'NONE',  ( 28.49999999999980105, -2.173586137069114521, -4.605770156576045160 ) ) ;
#105056=DIRECTION ( 'NONE',  ( -0.6830127018922180770, -0.6830127018922204085, -0.2588190451025213501 ) ) ;
#105057=CARTESIAN_POINT ( 'NONE',  ( -34.92500000000001137, -0.1833456135895722428, 4.500000000000000888 ) ) ;
#105060=VERTEX_POINT ( 'NONE', #9845 ) ;
#105061=VERTEX_POINT ( 'NONE', #9088 ) ;
#105063=VECTOR ( 'NONE', #131716, 1000.000000000000227 ) ;
#105064=ORIENTED_EDGE ( 'NONE', *, *, #3261, .F. ) ;
#105065=ADVANCED_FACE ( 'NONE', ( #53353 ), #120006, .F. ) ;
#105069=FACE_OUTER_BOUND ( 'NONE', #95636, .T. ) ;
#105070=AXIS2_PLACEMENT_3D ( 'NONE', #125993, #94748, #49865 ) ;
#105072=VERTEX_POINT ( 'NONE', #75840 ) ;
#105073=DIRECTION ( 'NONE',  ( 0.7071067811865486830, -0.7071067811865464625, -0.000000000000000000 ) ) ;
#105074=ORIENTED_EDGE ( 'NONE', *, *, #49283, .T. ) ;
#105075=LINE ( 'NONE', #36269, #40737 ) ;
#105076=EDGE_CURVE ( 'NONE', #135397, #89639, #54115, .T. ) ;
#105078=LINE ( 'NONE', #127553, #83263 ) ;
#105079=ORIENTED_EDGE ( 'NONE', *, *, #16835, .T. ) ;
#105080=VERTEX_POINT ( 'NONE', #381 ) ;
#105081=VERTEX_POINT ( 'NONE', #133095 ) ;
#105082=LINE ( 'NONE', #114525, #135128 ) ;
#105083=LINE ( 'NONE', #139170, #68588 ) ;
#105085=AXIS2_PLACEMENT_3D ( 'NONE', #40950, #65600, #53233 ) ;
#105088=VECTOR ( 'NONE', #79954, 1000.000000000000227 ) ;
#105089=ORIENTED_EDGE ( 'NONE', *, *, #70300, .T. ) ;
#105091=DIRECTION ( 'NONE',  ( 0.7071067811865486830, -0.7071067811865464625, -0.000000000000000000 ) ) ;
#105092=EDGE_CURVE ( 'NONE', #143140, #57564, #23581, .T. ) ;
#105093=ORIENTED_EDGE ( 'NONE', *, *, #83351, .T. ) ;
#105094=EDGE_LOOP ( 'NONE', ( #54051, #80230, #97210, #82806 ) ) ;
#105095=VECTOR ( 'NONE', #16906, 1000.000000000000000 ) ;
#105097=LINE ( 'NONE', #84102, #67358 ) ;
#105099=VERTEX_POINT ( 'NONE', #122902 ) ;
#105100=VECTOR ( 'NONE', #97104, 1000.000000000000227 ) ;
#105101=DIRECTION ( 'NONE',  ( 0.6830127018922181881, 0.6830127018922202975, -0.2588190451025214056 ) ) ;
#105102=EDGE_CURVE ( 'NONE', #71184, #103011, #56961, .T. ) ;
#105104=CARTESIAN_POINT ( 'NONE',  ( -19.49999999999986500, -17.91344420646044711, 1.358650452708419776 ) ) ;
#105105=DIRECTION ( 'NONE',  ( -0.3543493200069162685, -0.000000000000000000, -0.9351131265310288487 ) ) ;
#105106=ORIENTED_EDGE ( 'NONE', *, *, #42234, .T. ) ;
#105107=VECTOR ( 'NONE', #103052, 1000.000000000000000 ) ;
#105108=DIRECTION ( 'NONE',  ( 0.7071067811865486830, -0.7071067811865464625, -0.000000000000000000 ) ) ;
#105109=FACE_BOUND ( 'NONE', #60062, .T. ) ;
#105110=MECHANICAL_DESIGN_GEOMETRIC_PRESENTATION_REPRESENTATION('',(#112067),#884);
#105111=EDGE_LOOP ( 'NONE', ( #83927, #138209, #134599, #16975 ) ) ;
#105112=LINE ( 'NONE', #71798, #50454 ) ;
#105113=CARTESIAN_POINT ( 'NONE',  ( -54.18398860626899705, 28.73617430169825226, 5.000000000000000000 ) ) ;
#105114=EDGE_CURVE ( 'NONE', #80628, #9882, #112038, .T. ) ;
#105115=CARTESIAN_POINT ( 'NONE',  ( 57.18398860626899705, 28.73617430169827358, 5.000000000000000000 ) ) ;
#105116=ORIENTED_EDGE ( 'NONE', *, *, #95485, .T. ) ;
#105118=CARTESIAN_POINT ( 'NONE',  ( -19.01987774928536723, -17.24070752338410273, 20.23474786156464944 ) ) ;
#105119=VERTEX_POINT ( 'NONE', #92386 ) ;
#105121=ORIENTED_EDGE ( 'NONE', *, *, #85540, .F. ) ;
#105125=ORIENTED_EDGE ( 'NONE', *, *, #139305, .T. ) ;
#105126=CYLINDRICAL_SURFACE ( 'NONE', #22839, 0.5000000000000004441 ) ;
#105129=LINE ( 'NONE', #7207, #36638 ) ;
#105130=LINE ( 'NONE', #72561, #6467 ) ;
#105131=DIRECTION ( 'NONE',  ( 0.3543493200069162685, -0.000000000000000000, -0.9351131265310288487 ) ) ;
#105133=DIRECTION ( 'NONE',  ( -0.7071067811865486830, 0.7071067811865464625, 0.000000000000000000 ) ) ;
#105134=ADVANCED_FACE ( 'NONE', ( #12689 ), #134506, .F. ) ;
#105135=CARTESIAN_POINT ( 'NONE',  ( -33.48921356237309510, -27.52281430457078670, 5.000000000000000000 ) ) ;
#105136=CARTESIAN_POINT ( 'NONE',  ( 18.18398860626898994, 28.73617430169800002, 5.000000000000000000 ) ) ;
#105137=ORIENTED_EDGE ( 'NONE', *, *, #55831, .F. ) ;
#105138=ORIENTED_EDGE ( 'NONE', *, *, #125170, .T. ) ;
#105141=ORIENTED_EDGE ( 'NONE', *, *, #138047, .F. ) ;
#105142=CARTESIAN_POINT ( 'NONE',  ( 9.707013264292969623, -21.74070752338406365, 4.999753212805217117 ) ) ;
#105143=ORIENTED_EDGE ( 'NONE', *, *, #102941, .T. ) ;
#105144=ORIENTED_EDGE ( 'NONE', *, *, #139079, .T. ) ;
#105145=CARTESIAN_POINT ( 'NONE',  ( -34.92500000000001137, 22.22500000000000142, 4.000000000000000000 ) ) ;
#105146=DIRECTION ( 'NONE',  ( -0.7071067811865486830, -0.7071067811865464625, 0.000000000000000000 ) ) ;
#105147=EDGE_CURVE ( 'NONE', #114717, #72085, #25720, .T. ) ;
#105148=EDGE_CURVE ( 'NONE', #45162, #49422, #137358, .T. ) ;
#105150=ORIENTED_EDGE ( 'NONE', *, *, #57734, .T. ) ;
#105152=VERTEX_POINT ( 'NONE', #69249 ) ;
#105153=CARTESIAN_POINT ( 'NONE',  ( -2.999999999999983569, 7.931123077392109977, 4.000000000000000000 ) ) ;
#105154=FACE_OUTER_BOUND ( 'NONE', #130982, .T. ) ;
#105156=VERTEX_POINT ( 'NONE', #103970 ) ;
#105161=ORIENTED_EDGE ( 'NONE', *, *, #125319, .T. ) ;
#105162=ORIENTED_EDGE ( 'NONE', *, *, #25339, .F. ) ;
#105163=CARTESIAN_POINT ( 'NONE',  ( 0.000000000000000000, 0.000000000000000000, 5.000000000000000000 ) ) ;
#105164=ORIENTED_EDGE ( 'NONE', *, *, #41785, .T. ) ;
#105165=CARTESIAN_POINT ( 'NONE',  ( -41.01844734635645295, 18.75929247661552424, 20.33588619593452762 ) ) ;
#105166=CARTESIAN_POINT ( 'NONE',  ( 17.70025512860841488, -27.71228299555193786, 4.000000000000000000 ) ) ;
#105168=EDGE_CURVE ( 'NONE', #67630, #27153, #91692, .T. ) ;
#105170=ORIENTED_EDGE ( 'NONE', *, *, #98869, .F. ) ;
#105171=DIRECTION ( 'NONE',  ( -0.000000000000000000, -0.3543493200069152693, 0.9351131265310292928 ) ) ;
#105173=CARTESIAN_POINT ( 'NONE',  ( -8.671830600776411657, -0.7407075233842683737, 4.000000000000000000 ) ) ;
#105176=LINE ( 'NONE', #5834, #23957 ) ;
#105177=ORIENTED_EDGE ( 'NONE', *, *, #47870, .T. ) ;
#105178=CARTESIAN_POINT ( 'NONE',  ( 13.08100000000000307, 3.174999999999998046, 4.000000000000000000 ) ) ;
#105179=EDGE_LOOP ( 'NONE', ( #55188, #75810, #104662, #965 ) ) ;
#105180=ORIENTED_EDGE ( 'NONE', *, *, #90629, .T. ) ;
#105181=DIRECTION ( 'NONE',  ( -0.7071067811865487940, 0.7071067811865463515, 0.000000000000000000 ) ) ;
#105182=VECTOR ( 'NONE', #33500, 1000.000000000000000 ) ;
#105183=ORIENTED_EDGE ( 'NONE', *, *, #91318, .T. ) ;
#105184=PLANE ( 'NONE',  #67457 ) ;
#105185=LINE ( 'NONE', #73297, #142478 ) ;
#105186=AXIS2_PLACEMENT_3D ( 'NONE', #34823, #22471, #79068 ) ;
#105187=EDGE_CURVE ( 'NONE', #4701, #97256, #4614, .T. ) ;
#105188=CARTESIAN_POINT ( 'NONE',  ( -29.99999999999979039, -3.033600742197705369, 5.000000000000000000 ) ) ;
#105190=LINE ( 'NONE', #118182, #71615 ) ;
#105191=EDGE_CURVE ( 'NONE', #42001, #34223, #47532, .T. ) ;
#105192=VECTOR ( 'NONE', #30718, 999.9999999999998863 ) ;
#105193=CARTESIAN_POINT ( 'NONE',  ( -19.49999999999986500, 15.05218569542901541, 5.000000000000000000 ) ) ;
#105194=CARTESIAN_POINT ( 'NONE',  ( -25.82816939922334143, 21.75929247661549937, 4.000000000000000000 ) ) ;
#105195=CARTESIAN_POINT ( 'NONE',  ( 33.48921356237309510, -27.52281430457078670, 5.000000000000000000 ) ) ;
#105196=CARTESIAN_POINT ( 'NONE',  ( 0.000000000000000000, 0.000000000000000000, 5.000000000000000000 ) ) ;
#105197=CARTESIAN_POINT ( 'NONE',  ( -27.18398860626900060, 28.73617430169806042, 5.000000000000000000 ) ) ;
#105201=EDGE_CURVE ( 'NONE', #56830, #22851, #24300, .T. ) ;
#105202=EDGE_LOOP ( 'NONE', ( #102019, #14146, #41020, #30392 ) ) ;
#105203=ADVANCED_FACE ( 'NONE', ( #78684 ), #46824, .F. ) ;
#105204=ORIENTED_EDGE ( 'NONE', *, *, #129354, .T. ) ;
#105205=ORIENTED_EDGE ( 'NONE', *, *, #76119, .F. ) ;
#105207=VERTEX_POINT ( 'NONE', #15521 ) ;
#105208=AXIS2_PLACEMENT_3D ( 'NONE', #97686, #94804, #39772 ) ;
#105209=ORIENTED_EDGE ( 'NONE', *, *, #137713, .F. ) ;
#105210=ORIENTED_EDGE ( 'NONE', *, *, #80021, .F. ) ;
#105212=CARTESIAN_POINT ( 'NONE',  ( -6.511686059284278016, 6.759292476615653023, 16.35960578974471247 ) ) ;
#105214=DIRECTION ( 'NONE',  ( -0.7071067811865486830, -0.7071067811865464625, 0.000000000000000000 ) ) ;
#105215=DIRECTION ( 'NONE',  ( 0.7071067811865487940, 0.7071067811865463515, 0.000000000000000000 ) ) ;
#105217=FACE_OUTER_BOUND ( 'NONE', #35979, .T. ) ;
#105218=DIRECTION ( 'NONE',  ( 0.7071067811865487940, 0.7071067811865463515, 0.000000000000000000 ) ) ;
#105220=ORIENTED_EDGE ( 'NONE', *, *, #64070, .F. ) ;
#105222=CARTESIAN_POINT ( 'NONE',  ( 23.99999999999983302, -0.1606350220012988939, 4.664761815935144718 ) ) ;
#105223=DIRECTION ( 'NONE',  ( 0.7071067811865487940, 0.7071067811865463515, 0.000000000000000000 ) ) ;
#105224=DIRECTION ( 'NONE',  ( -0.000000000000000000, 0.3543493200069153248, 0.9351131265310292928 ) ) ;
#105226=LINE ( 'NONE', #50150, #12765 ) ;
#105228=LINE ( 'NONE', #8718, #86242 ) ;
#105231=EDGE_CURVE ( 'NONE', #133141, #15838, #8219, .T. ) ;
#105232=DIRECTION ( 'NONE',  ( -0.6830127018922181881, 0.6830127018922202975, -0.2588190451025214056 ) ) ;
#105233=VECTOR ( 'NONE', #133529, 1000.000000000000227 ) ;
#105235=ORIENTED_EDGE ( 'NONE', *, *, #9452, .T. ) ;
#105236=EDGE_LOOP ( 'NONE', ( #113940, #112147, #132410, #95278 ) ) ;
#105237=AXIS2_PLACEMENT_3D ( 'NONE', #104255, #4920, #62225 ) ;
#105239=ORIENTED_EDGE ( 'NONE', *, *, #128501, .F. ) ;
#105240=AXIS2_PLACEMENT_3D ( 'NONE', #112256, #68078, #13617 ) ;
#105241=DIRECTION ( 'NONE',  ( -1.000000000000000000, 0.000000000000000000, 0.000000000000000000 ) ) ;
#105242=CARTESIAN_POINT ( 'NONE',  ( -48.29974487139158867, -27.71228299555239971, 4.000000000000000000 ) ) ;
#105243=EDGE_CURVE ( 'NONE', #61782, #102663, #106105, .T. ) ;
#105244=DIRECTION ( 'NONE',  ( 0.6830127018922180770, -0.6830127018922204085, -0.2588190451025213501 ) ) ;
#105246=CARTESIAN_POINT ( 'NONE',  ( -51.48921356237309510, -27.52281430457091460, 5.000000000000000000 ) ) ;
#105247=DIRECTION ( 'NONE',  ( -0.7071067811865486830, 0.7071067811865464625, 0.000000000000000000 ) ) ;
#105249=ORIENTED_EDGE ( 'NONE', *, *, #83420, .F. ) ;
#105251=ORIENTED_EDGE ( 'NONE', *, *, #70594, .T. ) ;
#105252=ADVANCED_FACE ( 'NONE', ( #84417 ), #73529, .F. ) ;
#105253=CARTESIAN_POINT ( 'NONE',  ( -27.79289321881326558, -20.24070752338407431, 5.000000000000000000 ) ) ;
#105254=FACE_OUTER_BOUND ( 'NONE', #65325, .T. ) ;
#105256=PLANE ( 'NONE',  #71942 ) ;
#105260=DIRECTION ( 'NONE',  ( 1.000000000000000000, 0.000000000000000000, 0.000000000000000000 ) ) ;
#105261=LINE ( 'NONE', #84939, #57765 ) ;
#105262=DIRECTION ( 'NONE',  ( -0.7071067811865486830, 0.7071067811865464625, 0.000000000000000000 ) ) ;
#105263=ADVANCED_FACE ( 'NONE', ( #95257 ), #7520, .T. ) ;
#105264=EDGE_CURVE ( 'NONE', #3523, #139938, #51781, .T. ) ;
#105268=ORIENTED_EDGE ( 'NONE', *, *, #3227, .T. ) ;
#105269=DIRECTION ( 'NONE',  ( -0.000000000000000000, 0.000000000000000000, 1.000000000000000000 ) ) ;
#105270=CARTESIAN_POINT ( 'NONE',  ( 34.49999999999976552, -4.535744391599457082, 4.994342998332164107 ) ) ;
#105271=ORIENTED_EDGE ( 'NONE', *, *, #16681, .F. ) ;
#105272=VERTEX_POINT ( 'NONE', #106842 ) ;
#105274=ORIENTED_EDGE ( 'NONE', *, *, #114205, .T. ) ;
#105275=VECTOR ( 'NONE', #25408, 1000.000000000000000 ) ;
#105277=VERTEX_POINT ( 'NONE', #72855 ) ;
#105279=CARTESIAN_POINT ( 'NONE',  ( -21.48921356237309155, -27.52281430457070499, 5.000000000000000000 ) ) ;
#105280=FACE_BOUND ( 'NONE', #134070, .T. ) ;
#105281=CARTESIAN_POINT ( 'NONE',  ( -18.75860074219783868, 21.72500000000000853, 5.000000000000000000 ) ) ;
#105282=CARTESIAN_POINT ( 'NONE',  ( -54.48921356237310221, -27.52281430457093236, 5.000000000000000000 ) ) ;
#105283=LINE ( 'NONE', #138648, #119708 ) ;
#105284=ORIENTED_EDGE ( 'NONE', *, *, #27472, .F. ) ;
#105286=DIRECTION ( 'NONE',  ( -1.000000000000000000, 0.000000000000000000, -0.000000000000000000 ) ) ;
#105287=ORIENTED_EDGE ( 'NONE', *, *, #108935, .T. ) ;
#105288=ORIENTED_EDGE ( 'NONE', *, *, #127861, .T. ) ;
#105289=CARTESIAN_POINT ( 'NONE',  ( 6.938893903907228378E-15, -16.06887692260765377, 4.000000000000000000 ) ) ;
#105290=ORIENTED_EDGE ( 'NONE', *, *, #9673, .F. ) ;
#105291=VECTOR ( 'NONE', #116641, 1000.000000000000000 ) ;
#105292=ORIENTED_EDGE ( 'NONE', *, *, #4533, .F. ) ;
#105294=VERTEX_POINT ( 'NONE', #117010 ) ;
#105295=DIRECTION ( 'NONE',  ( 0.3543493200069162685, -0.000000000000000000, -0.9351131265310288487 ) ) ;
#105296=VECTOR ( 'NONE', #82778, 1000.000000000000000 ) ;
#105297=DIRECTION ( 'NONE',  ( -0.7071067811865486830, -0.7071067811865464625, 0.000000000000000000 ) ) ;
#105298=EDGE_CURVE ( 'NONE', #95984, #101438, #85099, .T. ) ;
#105299=EDGE_LOOP ( 'NONE', ( #7561, #40464, #67163, #129933 ) ) ;
#105301=DIRECTION ( 'NONE',  ( 0.000000000000000000, 0.3543493200069153248, 0.9351131265310291818 ) ) ;
#105302=CARTESIAN_POINT ( 'NONE',  ( -13.49999999999990408, 15.43112307739202294, 4.000000000000000000 ) ) ;
#105303=LINE ( 'NONE', #29175, #57430 ) ;
#105304=DIRECTION ( 'NONE',  ( -0.6830127018922181881, 0.6830127018922202975, -0.2588190451025214056 ) ) ;
#105305=PLANE ( 'NONE',  #108787 ) ;
#105306=ORIENTED_EDGE ( 'NONE', *, *, #83930, .T. ) ;
#105307=ORIENTED_EDGE ( 'NONE', *, *, #7093, .F. ) ;
#105308=CARTESIAN_POINT ( 'NONE',  ( 24.18398860626899705, 28.73617430169804265, 5.000000000000000000 ) ) ;
#105309=DIRECTION ( 'NONE',  ( 0.7071067811865487940, 0.7071067811865463515, 0.000000000000000000 ) ) ;
#105310=ORIENTED_EDGE ( 'NONE', *, *, #138410, .F. ) ;
#105311=EDGE_LOOP ( 'NONE', ( #129716, #129989, #108348, #71401 ) ) ;
#105312=ORIENTED_EDGE ( 'NONE', *, *, #135044, .F. ) ;
#105313=LINE ( 'NONE', #46156, #69874 ) ;
#105314=EDGE_CURVE ( 'NONE', #25822, #57637, #71383, .T. ) ;
#105315=ADVANCED_FACE ( 'NONE', ( #29996 ), #74235, .F. ) ;
#105318=CARTESIAN_POINT ( 'NONE',  ( -54.18398860626899705, 28.73617430169825226, 5.000000000000000000 ) ) ;
#105319=VECTOR ( 'NONE', #56946, 1000.000000000000000 ) ;
#105321=AXIS2_PLACEMENT_3D ( 'NONE', #37960, #49567, #25624 ) ;
#105323=CARTESIAN_POINT ( 'NONE',  ( -21.29974487139158512, -27.71228299555221142, 4.000000000000000000 ) ) ;
#105324=ORIENTED_EDGE ( 'NONE', *, *, #58519, .T. ) ;
#105325=VECTOR ( 'NONE', #36131, 1000.000000000000000 ) ;
#105326=EDGE_CURVE ( 'NONE', #59374, #52592, #60533, .T. ) ;
#105327=CARTESIAN_POINT ( 'NONE',  ( 41.99451991528749062, 28.92564299267967343, 4.000000000000000000 ) ) ;
#105328=FACE_OUTER_BOUND ( 'NONE', #103033, .T. ) ;
#105329=CARTESIAN_POINT ( 'NONE',  ( -5.999999999999950262, -13.44781430457068971, 5.000000000000000000 ) ) ;
#105330=EDGE_LOOP ( 'NONE', ( #121228, #86124, #10736, #88040 ) ) ;
#105331=PLANE ( 'NONE',  #77177 ) ;
#105332=ORIENTED_EDGE ( 'NONE', *, *, #142024, .T. ) ;
#105333=LINE ( 'NONE', #126371, #126045 ) ;
#105334=CARTESIAN_POINT ( 'NONE',  ( 0.000000000000000000, 0.000000000000000000, 5.000000000000000000 ) ) ;
#105336=EDGE_CURVE ( 'NONE', #84329, #121662, #38747, .T. ) ;
#105338=PLANE ( 'NONE',  #98122 ) ;
#105339=LINE ( 'NONE', #94459, #95139 ) ;
#105340=PLANE ( 'NONE',  #32847 ) ;
#105341=EDGE_LOOP ( 'NONE', ( #32940, #93383, #84142 ) ) ;
#105343=DIRECTION ( 'NONE',  ( -0.7071067811865486830, 0.7071067811865464625, 0.000000000000000000 ) ) ;
#105344=CARTESIAN_POINT ( 'NONE',  ( 34.42499999999998295, 22.22500000000000142, 0.4999999999999995559 ) ) ;
#105345=DIRECTION ( 'NONE',  ( -1.000000000000000000, 0.000000000000000000, 0.000000000000000000 ) ) ;
#105346=DIRECTION ( 'NONE',  ( 0.6830127018922181881, 0.6830127018922202975, -0.2588190451025214056 ) ) ;
#105347=DIRECTION ( 'NONE',  ( -0.000000000000000000, 0.3543493200069153248, 0.9351131265310292928 ) ) ;
#105348=ORIENTED_EDGE ( 'NONE', *, *, #36805, .F. ) ;
#105349=ORIENTED_EDGE ( 'NONE', *, *, #80473, .F. ) ;
#105350=DIRECTION ( 'NONE',  ( 0.6830127018922180770, -0.6830127018922204085, -0.2588190451025213501 ) ) ;
#105351=DIRECTION ( 'NONE',  ( 0.7071067811865487940, 0.7071067811865463515, -0.000000000000000000 ) ) ;
#105353=CARTESIAN_POINT ( 'NONE',  ( 17.20710678118642534, 15.75929247661555443, 5.000000000000000000 ) ) ;
#105354=DIRECTION ( 'NONE',  ( 1.000000000000000000, 0.000000000000000000, 0.000000000000000000 ) ) ;
#105355=CARTESIAN_POINT ( 'NONE',  ( 51.18398860626899705, 28.73617430169823095, 5.000000000000000000 ) ) ;
#105356=DIRECTION ( 'NONE',  ( -0.7071067811865487940, 0.7071067811865463515, -0.000000000000000000 ) ) ;
#105358=EDGE_CURVE ( 'NONE', #12779, #56087, #64072, .T. ) ;
#105359=FACE_OUTER_BOUND ( 'NONE', #63760, .T. ) ;
#105360=DIRECTION ( 'NONE',  ( 0.3543493200069162685, -0.000000000000000000, -0.9351131265310288487 ) ) ;
#105361=CARTESIAN_POINT ( 'NONE',  ( 12.48921356237309155, -27.52281430457064104, 5.000000000000000000 ) ) ;
#105362=FACE_OUTER_BOUND ( 'NONE', #765, .T. ) ;
#105364=CARTESIAN_POINT ( 'NONE',  ( -29.99999999999979039, 16.55218569542899587, 5.000000000000000000 ) ) ;
#105367=ORIENTED_EDGE ( 'NONE', *, *, #49108, .T. ) ;
#105368=DIRECTION ( 'NONE',  ( 0.7071067811865487940, -0.7071067811865463515, 0.000000000000000000 ) ) ;
#105370=ORIENTED_EDGE ( 'NONE', *, *, #101268, .T. ) ;
#105371=LINE ( 'NONE', #4574, #110317 ) ;
#105373=DIRECTION ( 'NONE',  ( 1.000000000000000000, 0.000000000000000000, 0.000000000000000000 ) ) ;
#105374=DIRECTION ( 'NONE',  ( 1.000000000000000000, -0.000000000000000000, -0.000000000000000000 ) ) ;
#105375=LINE ( 'NONE', #94495, #58003 ) ;
#105377=CARTESIAN_POINT ( 'NONE',  ( -13.49999999999990408, -16.53360074219757081, 5.000000000000000000 ) ) ;
#105378=DIRECTION ( 'NONE',  ( 0.6830127018922181881, 0.6830127018922202975, -0.2588190451025214056 ) ) ;
#105379=ORIENTED_EDGE ( 'NONE', *, *, #120073, .F. ) ;
#105380=ADVANCED_FACE ( 'NONE', ( #76384 ), #43742, .T. ) ;
#105381=CARTESIAN_POINT ( 'NONE',  ( -1.171830600776462061, 3.759292476615678336, 4.000000000000000000 ) ) ;
#105384=LINE ( 'NONE', #95943, #110340 ) ;
#105385=DIRECTION ( 'NONE',  ( -0.7071067811865486830, -0.7071067811865464625, 0.000000000000000000 ) ) ;
#105386=DIRECTION ( 'NONE',  ( 0.6830127018922181881, 0.6830127018922202975, -0.2588190451025214056 ) ) ;
#105389=DIRECTION ( 'NONE',  ( -0.7071067811865487940, 0.7071067811865463515, -0.000000000000000000 ) ) ;
#105391=VERTEX_POINT ( 'NONE', #119147 ) ;
#105394=LINE ( 'NONE', #17659, #26194 ) ;
#105396=CARTESIAN_POINT ( 'NONE',  ( 15.18398860626900237, 28.73617430169797871, 5.000000000000000000 ) ) ;
#105398=EDGE_CURVE ( 'NONE', #77014, #10464, #120548, .T. ) ;
#105400=VECTOR ( 'NONE', #39239, 1000.000000000000227 ) ;
#105401=CARTESIAN_POINT ( 'NONE',  ( 35.34328999833765295, 3.759292476615685441, 13.27625715073273582 ) ) ;
#105403=LINE ( 'NONE', #17669, #142899 ) ;
#105406=PLANE ( 'NONE',  #23793 ) ;
#105407=DIRECTION ( 'NONE',  ( -0.7071067811865486830, -0.7071067811865464625, 0.000000000000000000 ) ) ;
#105408=DIRECTION ( 'NONE',  ( -0.6830127018922180770, -0.6830127018922204085, -0.2588190451025213501 ) ) ;
#105409=LINE ( 'NONE', #6776, #102131 ) ;
#105410=CARTESIAN_POINT ( 'NONE',  ( 6.005480084712508493, 28.92564299267933947, 4.000000000000000000 ) ) ;
#105412=CARTESIAN_POINT ( 'NONE',  ( 36.29974487139159578, -27.71228299555231445, 4.000000000000000000 ) ) ;
#105413=FACE_OUTER_BOUND ( 'NONE', #40792, .T. ) ;
#105414=LINE ( 'NONE', #94535, #10050 ) ;
#105416=CARTESIAN_POINT ( 'NONE',  ( 8.010880286539427075, -22.02621442084248571, 4.990779571109219326 ) ) ;
#105417=VECTOR ( 'NONE', #39092, 999.9999999999998863 ) ;
#105418=EDGE_CURVE ( 'NONE', #22337, #36162, #19831, .T. ) ;
#105419=ORIENTED_EDGE ( 'NONE', *, *, #9579, .T. ) ;
#105421=VERTEX_POINT ( 'NONE', #87250 ) ;
#105423=FACE_OUTER_BOUND ( 'NONE', #48767, .T. ) ;
#105424=CARTESIAN_POINT ( 'NONE',  ( 14.20710678118644665, -14.24070752338414003, 5.000000000000000000 ) ) ;
#105425=CARTESIAN_POINT ( 'NONE',  ( -27.48921356237309155, -27.52281430457074762, 5.000000000000000000 ) ) ;
#105427=EDGE_LOOP ( 'NONE', ( #138714, #91383, #87163, #38400 ) ) ;
#105429=VECTOR ( 'NONE', #61543, 1000.000000000000000 ) ;
#105433=ORIENTED_EDGE ( 'NONE', *, *, #71221, .T. ) ;
#105434=ORIENTED_EDGE ( 'NONE', *, *, #37144, .T. ) ;
#105435=LINE ( 'NONE', #138085, #123141 ) ;
#105438=FACE_OUTER_BOUND ( 'NONE', #85263, .T. ) ;
#105439=FACE_BOUND ( 'NONE', #111130, .T. ) ;
#105441=CYLINDRICAL_SURFACE ( 'NONE', #2610, 0.5000000000000004441 ) ;
#105445=EDGE_LOOP ( 'NONE', ( #58103, #72320, #99230, #74176 ) ) ;
#105446=VERTEX_POINT ( 'NONE', #79817 ) ;
#105448=VERTEX_POINT ( 'NONE', #130781 ) ;
#105449=CARTESIAN_POINT ( 'NONE',  ( 30.18398860626900060, 28.73617430169808173, 5.000000000000000000 ) ) ;
#105450=ADVANCED_FACE ( 'NONE', ( #53936 ), #98131, .F. ) ;
#105451=DIRECTION ( 'NONE',  ( 0.7071067811865487940, 0.7071067811865463515, 0.000000000000000000 ) ) ;
#105452=CARTESIAN_POINT ( 'NONE',  ( -10.49999999999992539, -2.947814304570798960, 5.000000000000000000 ) ) ;
#105453=DIRECTION ( 'NONE',  ( -0.7071067811865487940, 0.7071067811865463515, -0.000000000000000000 ) ) ;
#105454=ORIENTED_EDGE ( 'NONE', *, *, #118743, .F. ) ;
#105455=DIRECTION ( 'NONE',  ( 0.000000000000000000, 1.000000000000000000, 0.000000000000000000 ) ) ;
#105456=LINE ( 'NONE', #6120, #101032 ) ;
#105457=FACE_OUTER_BOUND ( 'NONE', #115327, .T. ) ;
#105458=CARTESIAN_POINT ( 'NONE',  ( 5.999999999999960032, 1.931123077392165488, 4.000000000000000000 ) ) ;
#105459=DIRECTION ( 'NONE',  ( -0.000000000000000000, 0.000000000000000000, 1.000000000000000000 ) ) ;
#105462=DIRECTION ( 'NONE',  ( 0.7071067811865487940, 0.7071067811865463515, 0.000000000000000000 ) ) ;
#105464=LINE ( 'NONE', #115600, #130571 ) ;
#105465=( BOUNDED_CURVE ( )  B_SPLINE_CURVE ( 3, ( #82746, #38520, #126930, #5853 ),
 .UNSPECIFIED., .F., .T. ) 
 B_SPLINE_CURVE_WITH_KNOTS ( ( 4, 4 ),
 ( 5.043186909253407180, 5.074607125596362067 ),
 .UNSPECIFIED. ) 
 CURVE ( )  GEOMETRIC_REPRESENTATION_ITEM ( )  RATIONAL_B_SPLINE_CURVE ( ( 1.000000000000000000, 0.9999177325257868620, 0.9999177325257868620, 1.000000000000000000 ) ) 
 REPRESENTATION_ITEM ( '' )  );
#105466=DIRECTION ( 'NONE',  ( -0.7071067811865486830, 0.7071067811865464625, 0.000000000000000000 ) ) ;
#105468=ORIENTED_EDGE ( 'NONE', *, *, #58486, .T. ) ;
#105470=EDGE_CURVE ( 'NONE', #44113, #80548, #116665, .T. ) ;
#105471=EDGE_CURVE ( 'NONE', #23207, #69646, #25367, .T. ) ;
#105472=VERTEX_POINT ( 'NONE', #114518 ) ;
#105475=ADVANCED_FACE ( 'NONE', ( #82622 ), #37707, .F. ) ;
#105476=EDGE_CURVE ( 'NONE', #80926, #43625, #2902, .T. ) ;
#105480=EDGE_LOOP ( 'NONE', ( #62923, #37949, #13362, #54488 ) ) ;
#105481=AXIS2_PLACEMENT_3D ( 'NONE', #98490, #99926, #108617 ) ;
#105482=EDGE_CURVE ( 'NONE', #33763, #27758, #135624, .T. ) ;
#105484=ORIENTED_EDGE ( 'NONE', *, *, #88597, .T. ) ;
#105485=LINE ( 'NONE', #138865, #32564 ) ;
#105486=PLANE ( 'NONE',  #98402 ) ;
#105487=LINE ( 'NONE', #83047, #137402 ) ;
#105489=ORIENTED_EDGE ( 'NONE', *, *, #128422, .F. ) ;
#105490=CARTESIAN_POINT ( 'NONE',  ( -60.48921356237309510, -27.52281430457097500, 5.000000000000000000 ) ) ;
#105491=DIRECTION ( 'NONE',  ( -0.7071067811865487940, 0.7071067811865463515, -0.000000000000000000 ) ) ;
#105492=ADVANCED_FACE ( 'NONE', ( #48564 ), #27497, .F. ) ;
#105493=EDGE_LOOP ( 'NONE', ( #116143, #157, #108916, #141873 ) ) ;
#105494=PLANE ( 'NONE',  #15641 ) ;
#105495=ORIENTED_EDGE ( 'NONE', *, *, #42325, .F. ) ;
#105496=VERTEX_POINT ( 'NONE', #93496 ) ;
#105497=VERTEX_POINT ( 'NONE', #138430 ) ;
#105498=ORIENTED_EDGE ( 'NONE', *, *, #95589, .T. ) ;
#105499=LINE ( 'NONE', #17768, #137450 ) ;
#105500=EDGE_CURVE ( 'NONE', #7972, #78703, #105075, .T. ) ;
#105502=CARTESIAN_POINT ( 'NONE',  ( 27.18398860626900060, 28.73617430169806042, 5.000000000000000000 ) ) ;
#105503=LINE ( 'NONE', #83067, #131665 ) ;
#105508=DIRECTION ( 'NONE',  ( -0.6830127018922181881, 0.6830127018922202975, -0.2588190451025214056 ) ) ;
#105509=AXIS2_PLACEMENT_3D ( 'NONE', #20000, #109166, #76570 ) ;
#105511=CARTESIAN_POINT ( 'NONE',  ( 8.588385094051632862, 22.22500000000001208, 4.777194822843816802 ) ) ;
#105512=VECTOR ( 'NONE', #73364, 999.9999999999998863 ) ;
#105514=VECTOR ( 'NONE', #106885, 1000.000000000000000 ) ;
#105516=VERTEX_POINT ( 'NONE', #58787 ) ;
#105517=VECTOR ( 'NONE', #2138, 1000.000000000000000 ) ;
#105519=EDGE_CURVE ( 'NONE', #60169, #8640, #115198, .T. ) ;
#105520=ORIENTED_EDGE ( 'NONE', *, *, #100140, .T. ) ;
#105523=LINE ( 'NONE', #94646, #43016 ) ;
#105524=VECTOR ( 'NONE', #44050, 1000.000000000000000 ) ;
#105525=CARTESIAN_POINT ( 'NONE',  ( 34.92499999999998295, -21.72500000000000142, 5.000000000000000000 ) ) ;
#105529=EDGE_CURVE ( 'NONE', #92514, #127270, #102953, .T. ) ;
#105530=CARTESIAN_POINT ( 'NONE',  ( -24.48921356237309510, -27.52281430457072631, 5.000000000000000000 ) ) ;
#105531=DIRECTION ( 'NONE',  ( -0.000000000000000000, -0.3543493200069152693, 0.9351131265310292928 ) ) ;
#105532=LINE ( 'NONE', #6193, #115913 ) ;
#105533=EDGE_CURVE ( 'NONE', #18088, #31683, #34358, .T. ) ;
#105534=DIRECTION ( 'NONE',  ( -0.7071067811865486830, -0.7071067811865464625, -0.000000000000000000 ) ) ;
#105535=VERTEX_POINT ( 'NONE', #60170 ) ;
#105536=DIRECTION ( 'NONE',  ( 0.7071067811865487940, 0.7071067811865463515, 0.000000000000000000 ) ) ;
#105538=EDGE_CURVE ( 'NONE', #6466, #138961, #15194, .T. ) ;
#105539=DIRECTION ( 'NONE',  ( 0.3543493200069162685, -0.000000000000000000, -0.9351131265310288487 ) ) ;
#105540=CARTESIAN_POINT ( 'NONE',  ( 2.207106781186534139, 3.759292476615678336, 5.000000000000000000 ) ) ;
#105541=ORIENTED_EDGE ( 'NONE', *, *, #12605, .F. ) ;
#105542=CARTESIAN_POINT ( 'NONE',  ( -20.99999999999985789, -5.527737879153202805, -7.983877177622320076 ) ) ;
#105543=ORIENTED_EDGE ( 'NONE', *, *, #47581, .T. ) ;
#105544=ORIENTED_EDGE ( 'NONE', *, *, #27636, .F. ) ;
#105546=LINE ( 'NONE', #138202, #81528 ) ;
#105551=ORIENTED_EDGE ( 'NONE', *, *, #138606, .F. ) ;
#105552=ADVANCED_FACE ( 'NONE', ( #60913 ), #5737, .F. ) ;
#105553=LINE ( 'NONE', #139671, #132605 ) ;
#105554=DIRECTION ( 'NONE',  ( -0.000000000000000000, -0.3543493200069152693, 0.9351131265310292928 ) ) ;
#105556=DIRECTION ( 'NONE',  ( -0.7071067811865486830, -0.7071067811865464625, -0.000000000000000000 ) ) ;
#105557=AXIS2_PLACEMENT_3D ( 'NONE', #92542, #93986, #127330 ) ;
#105558=LINE ( 'NONE', #127324, #81562 ) ;
#105559=EDGE_LOOP ( 'NONE', ( #66242, #138193, #15732, #113120, #88330 ) ) ;
#105560=EDGE_CURVE ( 'NONE', #135168, #8423, #94186, .T. ) ;
#105561=DIRECTION ( 'NONE',  ( -0.000000000000000000, 0.000000000000000000, 1.000000000000000000 ) ) ;
#105562=EDGE_LOOP ( 'NONE', ( #126941, #28469, #58085, #30063 ) ) ;
#105564=PLANE ( 'NONE',  #128757 ) ;
#105567=ORIENTED_EDGE ( 'NONE', *, *, #60481, .T. ) ;
#105569=FACE_OUTER_BOUND ( 'NONE', #49393, .T. ) ;
#105570=CARTESIAN_POINT ( 'NONE',  ( 34.92499999999998295, 22.06445279868698250, 5.060837336147044674 ) ) ;
#105571=EDGE_CURVE ( 'NONE', #119991, #122630, #71050, .T. ) ;
#105572=FACE_OUTER_BOUND ( 'NONE', #107269, .T. ) ;
#105573=ORIENTED_EDGE ( 'NONE', *, *, #10075, .T. ) ;
#105574=FACE_OUTER_BOUND ( 'NONE', #113675, .T. ) ;
#105575=LINE ( 'NONE', #128092, #3656 ) ;
#105577=PLANE ( 'NONE',  #37675 ) ;
#105578=EDGE_LOOP ( 'NONE', ( #62096, #57518, #81101, #71425 ) ) ;
#105579=VECTOR ( 'NONE', #23638, 1000.000000000000000 ) ;
#105580=EDGE_CURVE ( 'NONE', #45800, #123719, #118802, .T. ) ;
#105583=VERTEX_POINT ( 'NONE', #128968 ) ;
#105587=CARTESIAN_POINT ( 'NONE',  ( -34.92500000000001137, 22.22500000000000142, 4.000000000000000000 ) ) ;
#105588=ORIENTED_EDGE ( 'NONE', *, *, #27709, .T. ) ;
#105589=CARTESIAN_POINT ( 'NONE',  ( -39.48921356237310221, -27.52281430457082934, 5.000000000000000000 ) ) ;
#105590=LINE ( 'NONE', #59987, #97621 ) ;
#105591=EDGE_CURVE ( 'NONE', #71076, #124824, #139157, .T. ) ;
#105592=VERTEX_POINT ( 'NONE', #51431 ) ;
#105594=LINE ( 'NONE', #140389, #76792 ) ;
#105596=FACE_OUTER_BOUND ( 'NONE', #75344, .T. ) ;
#105598=VERTEX_POINT ( 'NONE', #39858 ) ;
#105600=EDGE_CURVE ( 'NONE', #3235, #22619, #18027, .T. ) ;
#105601=LINE ( 'NONE', #94728, #47795 ) ;
#105602=CARTESIAN_POINT ( 'NONE',  ( -9.489213562373095101, -27.52281430457062328, 5.000000000000000000 ) ) ;
#105604=FACE_OUTER_BOUND ( 'NONE', #78529, .T. ) ;
#105605=VECTOR ( 'NONE', #13947, 1000.000000000000000 ) ;
#105606=AXIS2_PLACEMENT_3D ( 'NONE', #112584, #21293, #13242 ) ;
#105607=DIRECTION ( 'NONE',  ( -1.000000000000000000, 0.000000000000000000, 0.000000000000000000 ) ) ;
#105609=ORIENTED_EDGE ( 'NONE', *, *, #97649, .F. ) ;
#105611=ORIENTED_EDGE ( 'NONE', *, *, #91690, .T. ) ;
#105612=ORIENTED_EDGE ( 'NONE', *, *, #105833, .T. ) ;
#105613=ORIENTED_EDGE ( 'NONE', *, *, #42467, .F. ) ;
#105614=AXIS2_PLACEMENT_3D ( 'NONE', #97908, #98606, #33402 ) ;
#105617=EDGE_CURVE ( 'NONE', #5654, #63020, #107212, .T. ) ;
#105618=EDGE_LOOP ( 'NONE', ( #133409, #4996, #77322, #21370, #70718, #47572 ) ) ;
#105621=EDGE_CURVE ( 'NONE', #92540, #22430, #64426, .T. ) ;
#105622=DIRECTION ( 'NONE',  ( -0.000000000000000000, 0.3543493200069153248, 0.9351131265310292928 ) ) ;
#105623=CARTESIAN_POINT ( 'NONE',  ( 33.29974487139158867, -27.71228299555229313, 4.000000000000000000 ) ) ;
#105624=ORIENTED_EDGE ( 'NONE', *, *, #38437, .T. ) ;
#105625=CARTESIAN_POINT ( 'NONE',  ( 4.499999999999968914, 5.696342897626504254, -7.587980461218388761 ) ) ;
#105626=CARTESIAN_POINT ( 'NONE',  ( -57.48921356237308800, -27.52281430457095368, 5.000000000000000000 ) ) ;
#105627=EDGE_LOOP ( 'NONE', ( #91594, #115232, #101213, #52003 ) ) ;
#105629=EDGE_LOOP ( 'NONE', ( #19408, #31069, #85342, #58742 ) ) ;
#105630=ADVANCED_FACE ( 'NONE', ( #29639 ), #7885, .T. ) ;
#105633=ORIENTED_EDGE ( 'NONE', *, *, #28848, .F. ) ;
#105634=EDGE_LOOP ( 'NONE', ( #2323, #127431, #93095, #74494 ) ) ;
#105636=ORIENTED_EDGE ( 'NONE', *, *, #16970, .F. ) ;
#105637=( BOUNDED_CURVE ( )  B_SPLINE_CURVE ( 3, ( #45409, #122941, #65751, #143258 ),
 .UNSPECIFIED., .F., .T. ) 
 B_SPLINE_CURVE_WITH_KNOTS ( ( 4, 4 ),
 ( 1.901594255663603183, 1.933014472006537199 ),
 .UNSPECIFIED. ) 
 CURVE ( )  GEOMETRIC_REPRESENTATION_ITEM ( )  RATIONAL_B_SPLINE_CURVE ( ( 1.000000000000000000, 0.9999177325257868620, 0.9999177325257868620, 1.000000000000000000 ) ) 
 REPRESENTATION_ITEM ( '' )  );
#105639=ADVANCED_FACE ( 'NONE', ( #140550 ), #61611, .F. ) ;
#105640=PLANE ( 'NONE',  #37353 ) ;
#105642=LINE ( 'NONE', #140435, #72891 ) ;
#105643=EDGE_CURVE ( 'NONE', #119665, #137509, #105761, .T. ) ;
#105646=EDGE_CURVE ( 'NONE', #88426, #67057, #28953, .T. ) ;
#105647=DIRECTION ( 'NONE',  ( 0.7071067811865487940, -0.7071067811865463515, 0.000000000000000000 ) ) ;
#105648=CARTESIAN_POINT ( 'NONE',  ( -22.49999999999984368, -10.91253812416064228, 4.000000000000000000 ) ) ;
#105649=VECTOR ( 'NONE', #109154, 1000.000000000000000 ) ;
#105650=EDGE_CURVE ( 'NONE', #71933, #14462, #62307, .T. ) ;
#105655=ORIENTED_EDGE ( 'NONE', *, *, #140456, .F. ) ;
#105658=ORIENTED_EDGE ( 'NONE', *, *, #133816, .F. ) ;
#105660=DIRECTION ( 'NONE',  ( 0.7071067811865487940, 0.7071067811865463515, 0.000000000000000000 ) ) ;
#105661=VERTEX_POINT ( 'NONE', #119492 ) ;
#105662=CARTESIAN_POINT ( 'NONE',  ( 9.183988606268997046, 28.73617430169793607, 5.000000000000000000 ) ) ;
#105663=FACE_OUTER_BOUND ( 'NONE', #8973, .T. ) ;
#105664=EDGE_CURVE ( 'NONE', #47526, #20459, #50704, .T. ) ;
#105665=DIRECTION ( 'NONE',  ( -0.7071067811865486830, -0.7071067811865464625, 0.000000000000000000 ) ) ;
#105666=CARTESIAN_POINT ( 'NONE',  ( 34.92499999999998295, -5.993876922607981328, 4.000000000000000000 ) ) ;
#105667=EDGE_LOOP ( 'NONE', ( #37212, #119106, #127383, #38089 ) ) ;
#105668=EDGE_LOOP ( 'NONE', ( #124932, #64443, #75809, #87059 ) ) ;
#105669=EDGE_CURVE ( 'NONE', #22078, #115783, #94893, .T. ) ;
#105672=CARTESIAN_POINT ( 'NONE',  ( 12.98155265364323085, 18.75929247661552424, 20.33588619593440328 ) ) ;
#105673=DIRECTION ( 'NONE',  ( 0.7071067811865487940, 0.7071067811865463515, -0.000000000000000000 ) ) ;
#105674=VECTOR ( 'NONE', #18587, 1000.000000000000114 ) ;
#105675=CARTESIAN_POINT ( 'NONE',  ( -19.49999999999985434, 16.46639925780209168, 5.000000000000000000 ) ) ;
#105676=VERTEX_POINT ( 'NONE', #115662 ) ;
#105677=VERTEX_POINT ( 'NONE', #16356 ) ;
#105679=CARTESIAN_POINT ( 'NONE',  ( 31.19018167574429157, -18.74070752338409207, 7.910009926591434315 ) ) ;
#105680=LINE ( 'NONE', #48472, #62683 ) ;
#105682=CARTESIAN_POINT ( 'NONE',  ( 48.18398860626899705, 28.73617430169820608, 5.000000000000000000 ) ) ;
#105683=CARTESIAN_POINT ( 'NONE',  ( 36.48921356237310221, -27.52281430457080802, 5.000000000000000000 ) ) ;
#105684=EDGE_CURVE ( 'NONE', #83015, #90172, #50461, .T. ) ;
#105685=LINE ( 'NONE', #103553, #64793 ) ;
#105687=PLANE ( 'NONE',  #88343 ) ;
#105688=EDGE_CURVE ( 'NONE', #2187, #58967, #105523, .T. ) ;
#105689=VERTEX_POINT ( 'NONE', #37445 ) ;
#105690=LINE ( 'NONE', #117980, #62597 ) ;
#105691=CARTESIAN_POINT ( 'NONE',  ( -34.92500000000001137, -10.65190338184902252, -7.458287694568772608 ) ) ;
#105693=EDGE_CURVE ( 'NONE', #10862, #102959, #70801, .T. ) ;
#105695=LINE ( 'NONE', #73126, #99700 ) ;
#105696=ORIENTED_EDGE ( 'NONE', *, *, #98791, .F. ) ;
#105697=VECTOR ( 'NONE', #141654, 999.9999999999998863 ) ;
#105698=CARTESIAN_POINT ( 'NONE',  ( -33.48921356237309510, -27.52281430457078670, 5.000000000000000000 ) ) ;
#105699=LINE ( 'NONE', #17967, #129517 ) ;
#105700=ORIENTED_EDGE ( 'NONE', *, *, #20735, .F. ) ;
#105701=CARTESIAN_POINT ( 'NONE',  ( -22.49999999999982947, 13.08746187583911080, 4.000000000000000000 ) ) ;
#105702=EDGE_LOOP ( 'NONE', ( #11748, #81326, #77991, #124581 ) ) ;
#105704=VECTOR ( 'NONE', #10225, 1000.000000000000227 ) ;
#105706=AXIS2_PLACEMENT_3D ( 'NONE', #77100, #78502, #32134 ) ;
#105709=LINE ( 'NONE', #96254, #131635 ) ;
#105710=EDGE_CURVE ( 'NONE', #106925, #71937, #48304, .T. ) ;
#105711=LINE ( 'NONE', #93445, #14389 ) ;
#105712=CARTESIAN_POINT ( 'NONE',  ( 11.29289321881338282, -6.740707523384211086, 5.000000000000000000 ) ) ;
#105713=DIRECTION ( 'NONE',  ( -0.7071067811865486830, 0.7071067811865464625, 0.000000000000000000 ) ) ;
#105716=CARTESIAN_POINT ( 'NONE',  ( 26.29289321881326913, 2.259292476615694323, 5.000000000000000000 ) ) ;
#105717=AXIS2_PLACEMENT_3D ( 'NONE', #77441, #54263, #98443 ) ;
#105718=DIRECTION ( 'NONE',  ( -0.7071067811865487940, 0.7071067811865463515, -0.000000000000000000 ) ) ;
#105719=DIRECTION ( 'NONE',  ( 0.6830127018922180770, -0.6830127018922204085, -0.2588190451025213501 ) ) ;
#105721=ORIENTED_EDGE ( 'NONE', *, *, #73695, .T. ) ;
#105724=EDGE_LOOP ( 'NONE', ( #101883, #44109, #115995, #51197 ) ) ;
#105727=DIRECTION ( 'NONE',  ( 0.7071067811865486830, -0.7071067811865464625, -0.000000000000000000 ) ) ;
#105728=PLANE ( 'NONE',  #10812 ) ;
#105729=ORIENTED_EDGE ( 'NONE', *, *, #31283, .T. ) ;
#105730=DIRECTION ( 'NONE',  ( 0.7071067811865487940, 0.7071067811865463515, 0.000000000000000000 ) ) ;
#105732=LINE ( 'NONE', #84726, #136653 ) ;
#105733=CARTESIAN_POINT ( 'NONE',  ( -34.92500000000001137, 6.006123077391876564, 4.000000000000000000 ) ) ;
#105734=ADVANCED_FACE ( 'NONE', ( #117117 ), #59914, .F. ) ;
#105735=FACE_OUTER_BOUND ( 'NONE', #85212, .T. ) ;
#105736=CARTESIAN_POINT ( 'NONE',  ( -21.29974487139158512, -27.71228299555221142, 4.000000000000000000 ) ) ;
#105739=PLANE ( 'NONE',  #74773 ) ;
#105740=DIRECTION ( 'NONE',  ( -0.3543493200069162685, -0.000000000000000000, -0.9351131265310288487 ) ) ;
#105741=CARTESIAN_POINT ( 'NONE',  ( 0.000000000000000000, 21.72500000000000142, 0.000000000000000000 ) ) ;
#105742=DIRECTION ( 'NONE',  ( -0.6830127018922180770, -0.6830127018922204085, -0.2588190451025213501 ) ) ;
#105743=EDGE_CURVE ( 'NONE', #47934, #3210, #125147, .T. ) ;
#105744=ORIENTED_EDGE ( 'NONE', *, *, #142856, .F. ) ;
#105747=VECTOR ( 'NONE', #70003, 999.9999999999998863 ) ;
#105748=ORIENTED_EDGE ( 'NONE', *, *, #41116, .T. ) ;
#105749=PLANE ( 'NONE',  #27026 ) ;
#105751=DIRECTION ( 'NONE',  ( -0.000000000000000000, -0.3543493200069152693, 0.9351131265310292928 ) ) ;
#105752=ORIENTED_EDGE ( 'NONE', *, *, #115461, .F. ) ;
#105754=DIRECTION ( 'NONE',  ( -0.7071067811865486830, 0.7071067811865464625, 0.000000000000000000 ) ) ;
#105757=ADVANCED_FACE ( 'NONE', ( #136729 ), #70112, .F. ) ;
#105758=VERTEX_POINT ( 'NONE', #93946 ) ;
#105759=DIRECTION ( 'NONE',  ( 0.6830127018922180770, -0.6830127018922204085, -0.2588190451025213501 ) ) ;
#105760=EDGE_LOOP ( 'NONE', ( #142064, #71494, #93136, #22814 ) ) ;
#105761=LINE ( 'NONE', #95623, #19897 ) ;
#105762=AXIS2_PLACEMENT_3D ( 'NONE', #119629, #87750, #129100 ) ;
#105763=LINE ( 'NONE', #50705, #74646 ) ;
#105764=PLANE ( 'NONE',  #82471 ) ;
#105765=DIRECTION ( 'NONE',  ( 0.7071067811865487940, 0.7071067811865463515, 0.000000000000000000 ) ) ;
#105766=EDGE_LOOP ( 'NONE', ( #19316, #138494, #74145, #82418 ) ) ;
#105767=ORIENTED_EDGE ( 'NONE', *, *, #89668, .F. ) ;
#105768=VECTOR ( 'NONE', #16854, 1000.000000000000000 ) ;
#105769=VERTEX_POINT ( 'NONE', #38864 ) ;
#105770=CARTESIAN_POINT ( 'NONE',  ( -18.83829387547368484, -6.740707523384205757, 16.75550250614862691 ) ) ;
#105771=ADVANCED_FACE ( 'NONE', ( #4737 ), #104824, .F. ) ;
#105772=DIRECTION ( 'NONE',  ( 0.6830127018922181881, 0.6830127018922202975, -0.2588190451025214056 ) ) ;
#105774=DIRECTION ( 'NONE',  ( -0.7071067811865487940, 0.7071067811865463515, -0.000000000000000000 ) ) ;
#105775=VECTOR ( 'NONE', #34348, 999.9999999999998863 ) ;
#105777=VECTOR ( 'NONE', #135942, 1000.000000000000000 ) ;
#105778=ORIENTED_EDGE ( 'NONE', *, *, #49147, .F. ) ;
#105779=DIRECTION ( 'NONE',  ( 0.3543493200069163240, 0.000000000000000000, -0.9351131265310288487 ) ) ;
#105780=ORIENTED_EDGE ( 'NONE', *, *, #91930, .F. ) ;
#105781=ORIENTED_EDGE ( 'NONE', *, *, #130879, .T. ) ;
#105783=DIRECTION ( 'NONE',  ( -0.000000000000000000, -0.3543493200069152693, 0.9351131265310292928 ) ) ;
#105784=DIRECTION ( 'NONE',  ( -0.7071067811865486830, -0.7071067811865464625, -0.000000000000000000 ) ) ;
#105785=ORIENTED_EDGE ( 'NONE', *, *, #75065, .F. ) ;
#105788=DIRECTION ( 'NONE',  ( -0.7071067811865486830, -0.7071067811865464625, -0.000000000000000000 ) ) ;
#105789=CARTESIAN_POINT ( 'NONE',  ( -54.18398860626899705, 28.73617430169825226, 5.000000000000000000 ) ) ;
#105790=LINE ( 'NONE', #84110, #4888 ) ;
#105791=ORIENTED_EDGE ( 'NONE', *, *, #31961, .T. ) ;
#105792=CARTESIAN_POINT ( 'NONE',  ( -12.29974487139158512, -27.71228299555214747, 4.000000000000000000 ) ) ;
#105793=VECTOR ( 'NONE', #37543, 999.9999999999998863 ) ;
#105795=VERTEX_POINT ( 'NONE', #6185 ) ;
#105796=DIRECTION ( 'NONE',  ( -0.000000000000000000, 0.3543493200069153248, 0.9351131265310292928 ) ) ;
#105797=FACE_OUTER_BOUND ( 'NONE', #24153, .T. ) ;
#105798=EDGE_CURVE ( 'NONE', #126032, #142844, #81683, .T. ) ;
#105799=EDGE_LOOP ( 'NONE', ( #5097, #115586, #11909, #61285 ) ) ;
#105800=LINE ( 'NONE', #50746, #50578 ) ;
#105801=ORIENTED_EDGE ( 'NONE', *, *, #116396, .T. ) ;
#105802=VERTEX_POINT ( 'NONE', #93236 ) ;
#105803=VECTOR ( 'NONE', #109186, 1000.000000000000000 ) ;
#105804=ORIENTED_EDGE ( 'NONE', *, *, #16345, .F. ) ;
#105805=VECTOR ( 'NONE', #44897, 1000.000000000000000 ) ;
#105807=EDGE_CURVE ( 'NONE', #48148, #121857, #33806, .T. ) ;
#105809=CARTESIAN_POINT ( 'NONE',  ( -8.999999999999937828, 17.96639925780208102, 5.000000000000000000 ) ) ;
#105811=ADVANCED_FACE ( 'NONE', ( #26558 ), #106223, .F. ) ;
#105812=DIRECTION ( 'NONE',  ( -0.7071067811865487940, 0.7071067811865463515, -0.000000000000000000 ) ) ;
#105813=CARTESIAN_POINT ( 'NONE',  ( 0.005480084712502889671, 28.92564299267938210, 4.000000000000000000 ) ) ;
#105814=EDGE_CURVE ( 'NONE', #18168, #93700, #63592, .T. ) ;
#105815=PLANE ( 'NONE',  #6479 ) ;
#105816=DIRECTION ( 'NONE',  ( 1.000000000000000000, 0.000000000000000000, 0.000000000000000000 ) ) ;
#105817=VECTOR ( 'NONE', #52289, 1000.000000000000114 ) ;
#105818=EDGE_CURVE ( 'NONE', #106471, #37562, #33115, .T. ) ;
#105819=LINE ( 'NONE', #86254, #116285 ) ;
#105820=DIRECTION ( 'NONE',  ( 0.6830127018922180770, -0.6830127018922204085, -0.2588190451025213501 ) ) ;
#105822=DIRECTION ( 'NONE',  ( -0.7071067811865486830, -0.7071067811865464625, 0.000000000000000000 ) ) ;
#105823=ADVANCED_FACE ( 'NONE', ( #121488 ), #130259, .F. ) ;
#105824=ORIENTED_EDGE ( 'NONE', *, *, #78055, .T. ) ;
#105826=ORIENTED_EDGE ( 'NONE', *, *, #60228, .F. ) ;
#105827=VERTEX_POINT ( 'NONE', #96154 ) ;
#105829=EDGE_LOOP ( 'NONE', ( #26640, #83729, #97603, #53494 ) ) ;
#105830=ORIENTED_EDGE ( 'NONE', *, *, #40251, .T. ) ;
#105831=LINE ( 'NONE', #86271, #12070 ) ;
#105832=DIRECTION ( 'NONE',  ( -0.7071067811865487940, 0.7071067811865463515, -0.000000000000000000 ) ) ;
#105833=EDGE_CURVE ( 'NONE', #5100, #56149, #65006, .T. ) ;
#105834=EDGE_CURVE ( 'NONE', #87449, #12661, #41806, .T. ) ;
#105835=CARTESIAN_POINT ( 'NONE',  ( -24.70701326429287903, -21.74070752338406365, 4.999753212805221558 ) ) ;
#105837=AXIS2_PLACEMENT_3D ( 'NONE', #55972, #121181, #66821 ) ;
#105838=CARTESIAN_POINT ( 'NONE',  ( -10.78678096696635436, 12.75929247661558996, 10.29404684609032827 ) ) ;
#105839=ORIENTED_EDGE ( 'NONE', *, *, #80588, .T. ) ;
#105840=ADVANCED_FACE ( 'NONE', ( #41084 ), #10571, .F. ) ;
#105841=DIRECTION ( 'NONE',  ( 0.7071067811865486830, -0.7071067811865464625, -0.000000000000000000 ) ) ;
#105842=DIRECTION ( 'NONE',  ( -0.7071067811865486830, 0.7071067811865464625, 0.000000000000000000 ) ) ;
#105845=ORIENTED_EDGE ( 'NONE', *, *, #136588, .F. ) ;
#105849=ORIENTED_EDGE ( 'NONE', *, *, #30753, .T. ) ;
#105850=ORIENTED_EDGE ( 'NONE', *, *, #77287, .F. ) ;
#105851=PLANE ( 'NONE',  #991 ) ;
#105852=ORIENTED_EDGE ( 'NONE', *, *, #97999, .T. ) ;
#105854=DIRECTION ( 'NONE',  ( -0.7071067811865487940, 0.7071067811865463515, -0.000000000000000000 ) ) ;
#105855=DIRECTION ( 'NONE',  ( 0.7071067811865486830, -0.7071067811865464625, -0.000000000000000000 ) ) ;
#105856=DIRECTION ( 'NONE',  ( 1.000000000000000000, 0.000000000000000000, 0.000000000000000000 ) ) ;
#105858=( BOUNDED_CURVE ( )  B_SPLINE_CURVE ( 3, ( #86780, #140425, #111922, #96882 ),
 .UNSPECIFIED., .F., .F. ) 
 B_SPLINE_CURVE_WITH_KNOTS ( ( 4, 4 ),
 ( 3.996889577052295195, 4.025035655492697373 ),
 .UNSPECIFIED. ) 
 CURVE ( )  GEOMETRIC_REPRESENTATION_ITEM ( )  RATIONAL_B_SPLINE_CURVE ( ( 1.000000000000000000, 0.9999339842785831545, 0.9999339842785831545, 1.000000000000000000 ) ) 
 REPRESENTATION_ITEM ( '' )  );
#105859=ORIENTED_EDGE ( 'NONE', *, *, #43851, .F. ) ;
#105861=DIRECTION ( 'NONE',  ( 0.7071067811865486830, -0.7071067811865464625, -0.000000000000000000 ) ) ;
#105862=CARTESIAN_POINT ( 'NONE',  ( -17.70025512860841488, -27.71228299555193786, 4.000000000000000000 ) ) ;
#105863=ADVANCED_FACE ( 'NONE', ( #43246 ), #62866, .F. ) ;
#105866=CARTESIAN_POINT ( 'NONE',  ( 24.18398860626899705, 28.73617430169804265, 5.000000000000000000 ) ) ;
#105867=LINE ( 'NONE', #40654, #9862 ) ;
#105868=ORIENTED_EDGE ( 'NONE', *, *, #50463, .T. ) ;
#105870=ORIENTED_EDGE ( 'NONE', *, *, #84406, .F. ) ;
#105871=VERTEX_POINT ( 'NONE', #99015 ) ;
#105872=CARTESIAN_POINT ( 'NONE',  ( 34.92499999999998295, -12.18334561358941137, 4.500000000000000888 ) ) ;
#105873=DIRECTION ( 'NONE',  ( -0.6830127018922180770, -0.6830127018922204085, -0.2588190451025213501 ) ) ;
#105875=FACE_OUTER_BOUND ( 'NONE', #41947, .T. ) ;
#105877=CARTESIAN_POINT ( 'NONE',  ( 54.48921356237310221, -27.52281430457093236, 5.000000000000000000 ) ) ;
#105878=CARTESIAN_POINT ( 'NONE',  ( -21.29974487139158512, -27.71228299555221142, 4.000000000000000000 ) ) ;
#105879=VECTOR ( 'NONE', #61132, 1000.000000000000000 ) ;
#105880=CARTESIAN_POINT ( 'NONE',  ( -39.18398860626899705, 28.73617430169814568, 5.000000000000000000 ) ) ;
#105881=CARTESIAN_POINT ( 'NONE',  ( -31.82816939922330945, 21.75929247661549937, 4.000000000000000000 ) ) ;
#105882=ADVANCED_FACE ( 'NONE', ( #52667, #64271, #30203, #30947, #96852, #141095, #74451, #109908, #119336, #53386, #7724, #19335, #107750, #8409, #142558, #86750, #97592, #9876, #130971, #42547, #31647, #75868, #54837, #109191, #131676, #32360, #76603, #54146, #120031, #98336, #120775, #143253, #43952, #88173, #67883, #66425, #34496, #124358, #135941, #33800, #13420, #80168, #35951, #91044, #123674, #68575, #1126, #25027, #22864, #57702, #3272, #45404, #56296, #47563, #91720, #69279, #2549, #101165, #46856, #78014, #135266, #55549, #122192, #78719, #410, #36623, #56992, #133810, #122934, #80872, #101887, #24328, #22164, #23612, #112068, #67131, #112762, #113463, #14154, #134542, #12724, #1808, #110595, #111324, #90290, #58445, #102625, #89579, #11274, #99741, #44711, #88902, #133122, #12007, #100478, #46110, #35238, #79483, #138093, #95289, #103298, #3946, #17028, #60566, #117039, #106134, #127198, #126479, #6097, #17706, #93156, #114188, #38780, #48221, #72886, #139552, #127945, #82300, #104740, #61297, #61979, #5403, #27896, #105439, #15547, #136649, #92416, #40233, #6810, #50375, #125064, #94564, #49683, #27172, #25751, #72162, #93861, #70020, #14872, #37357, #83005, #138819, #51095, #81593, #116334, #39514, #59146, #83744, #28635, #125800, #26474, #70724, #114870, #59830, #71417, #103994, #115571, #4655, #48956, #16267, #137387, #38079, #130077, #75004, #73556, #97413, #131503, #107590, #84448, #118464, #10407, #9699, #8248, #74272, #87284, #21310, #128642, #109005, #142389, #98160, #53965, #62688, #7551, #63423, #51813, #30776, #96683, #65568, #42369, #85840, #19163, #43079, #30023, #19863, #8941, #32185, #52496, #95995, #117724, #140239, #140928, #76419, #29315, #106870, #86581, #120587, #64099, #119178, #108269, #41622, #75698, #109737, #53205, #31477, #141669, #64825, #119867, #130810, #20572, #98850, #40925, #54666, #129340, #143084, #18410, #85128, #56837, #22689, #13969, #110428, #57529, #11102, #58274, #77835, #101717, #132239, #100304, #66253, #87989, #133647, #55379, #956, #22003, #89415, #34324, #32931, #100996, #90870, #66962, #43776, #122021, #90121, #111139, #80009, #99553, #78553, #122752, #77151, #1652, #135102, #11831, #121321, #56113, #134366, #45935, #23436, #67708, #225, #45238, #2367, #102460, #44527, #35068, #88727, #132957, #111893, #33637, #24867, #12556, #79308, #123509, #24162, #69110, #68418, #112600, #113292, #13257, #46688, #35788, #124186, #27719, #58987, #71976, #135780, #5234, #103143, #93704, #82144, #126322, #49520, #127023, #28459, #38610, #104572, #72719, #103823, #15383, #48066, #137929, #82841, #5933, #115403, #137217, #61131, #70566, #60386, #50208, #116162, #16858, #127770, #3783, #81432, #36468, #94397, #136479, #4475, #91563, #116872, #17545, #92249, #105280, #27007, #114711, #138645, #71253, #3109, #59668, #48781, #39339, #92988, #37174, #83558, #16094, #47397, #37914, #61808, #124899, #80702, #25572, #69847, #114021, #14710, #26309, #125632, #140079, #8767, #84960, #142222, #108104, #139384, #32003, #64638, #76236, #117556, #97223, #120398, #51637, #129166, #6634, #87106, #84285, #141488, #41444, #97983, #131321, #53027, #107421, #130637, #42908, #74092, #95110, #85656, #31305, #18236, #75521, #40067, #42194, #62517, #86408, #129892, #30603, #119690, #20391, #40756, #106684, #73392, #21122, #105968, #108819, #50919, #9505, #53786, #128479, #74832, #96511, #29151, #29850, #19693, #7378, #95830, #118282, #18990, #63255, #119011, #8081, #52324, #140750, #63933, #134926, #78376, #112426, #35616, #43592, #132052, #44339, #32741, #110961, #77671, #46506, #23244, #66784, #99372, #34884, #10930, #778, #133472, #79121, #39, #76976, #98678, #121143, #1483, #13082, #65385, #87809, #67521, #89937, #45072, #11644, #55924, #88552, #56666, #134187, #132784, #12382, #34159, #45771, #100829, #122568, #100129, #79844, #21841, #111714, #110252, #121841, #123327, #66084, #23990, #33470, #124020, #55198, #68251, #22523, #109563, #89246, #57356, #10238, #101532, #2186, #54498, #90692, #142908, #114550, #102284, #14538, #93528, #102980, #26833, #48596, #38439, #137762, #124723, #92078, #68946, #71083, #94227, #82661, #136306, #58817, #27532, #105109, #39152, #126844, #115227, #37738, #13789, #71796, #3616, #125450, #113119, #138467, #83374, #69664, #104383, #92799, #36992, #15912, #137031, #24689, #81246, #26134, #115964, #60203, #16667, #5044, #60953, #126162, #4295, #58084, #70400, #49345, #81973, #15217, #59496, #2935, #103651, #5770, #47229, #36298, #50035, #91403, #135611, #80527, #25392, #113842, #47912, #50740, #29675, #139910, #110617, #85480, #128998, #18058, #99036, #73220, #63071, #52158, #143271, #62347, #94930, #17384 ), #73915, .F. ) ;
#105883=FACE_OUTER_BOUND ( 'NONE', #139259, .T. ) ;
#105884=LINE ( 'NONE', #141394, #114196 ) ;
#105886=DIRECTION ( 'NONE',  ( -0.3543493200069162685, -0.000000000000000000, -0.9351131265310288487 ) ) ;
#105887=CARTESIAN_POINT ( 'NONE',  ( -29.99999999999979039, -16.06887692260765377, 4.000000000000000000 ) ) ;
#105888=DIRECTION ( 'NONE',  ( -0.7071067811865487940, 0.7071067811865463515, 0.000000000000000000 ) ) ;
#105889=VERTEX_POINT ( 'NONE', #107244 ) ;
#105890=ORIENTED_EDGE ( 'NONE', *, *, #63957, .F. ) ;
#105891=ORIENTED_EDGE ( 'NONE', *, *, #94539, .F. ) ;
#105893=AXIS2_PLACEMENT_3D ( 'NONE', #108940, #53142, #121263 ) ;
#105896=ADVANCED_FACE ( 'NONE', ( #74650 ), #117385, .F. ) ;
#105897=ORIENTED_EDGE ( 'NONE', *, *, #32210, .T. ) ;
#105899=FACE_OUTER_BOUND ( 'NONE', #76363, .T. ) ;
#105900=ORIENTED_EDGE ( 'NONE', *, *, #45285, .T. ) ;
#105901=VECTOR ( 'NONE', #47090, 1000.000000000000000 ) ;
#105902=CARTESIAN_POINT ( 'NONE',  ( 63.48921356237309510, -27.52281430457099631, 5.000000000000000000 ) ) ;
#105903=PLANE ( 'NONE',  #2462 ) ;
#105908=EDGE_CURVE ( 'NONE', #86644, #12213, #7188, .T. ) ;
#105909=ORIENTED_EDGE ( 'NONE', *, *, #87695, .F. ) ;
#105912=LINE ( 'NONE', #6578, #114498 ) ;
#105913=CARTESIAN_POINT ( 'NONE',  ( -29.99451991528749417, 28.92564299267958816, 4.000000000000000000 ) ) ;
#105914=LINE ( 'NONE', #10012, #40542 ) ;
#105916=LINE ( 'NONE', #95054, #130229 ) ;
#105917=LINE ( 'NONE', #5168, #82474 ) ;
#105918=AXIS2_PLACEMENT_3D ( 'NONE', #51643, #31311, #86414 ) ;
#105920=DIRECTION ( 'NONE',  ( 0.6830127018922181881, 0.6830127018922202975, -0.2588190451025214056 ) ) ;
#105921=VECTOR ( 'NONE', #126633, 1000.000000000000000 ) ;
#105924=ORIENTED_EDGE ( 'NONE', *, *, #77324, .F. ) ;
#105926=ORIENTED_EDGE ( 'NONE', *, *, #111117, .T. ) ;
#105927=DIRECTION ( 'NONE',  ( 1.000000000000000000, 0.000000000000000000, 0.000000000000000000 ) ) ;
#105928=CARTESIAN_POINT ( 'NONE',  ( 36.29974487139159578, -27.71228299555231445, 4.000000000000000000 ) ) ;
#105929=AXIS2_PLACEMENT_3D ( 'NONE', #112052, #135248, #78700 ) ;
#105930=LINE ( 'NONE', #6593, #110469 ) ;
#105931=CARTESIAN_POINT ( 'NONE',  ( -26.99999999999980815, 1.761378380278660227, -6.096875308897316437 ) ) ;
#105932=DIRECTION ( 'NONE',  ( 0.7071067811865487940, -0.7071067811865463515, 0.000000000000000000 ) ) ;
#105933=CARTESIAN_POINT ( 'NONE',  ( 33.79289321881321229, -2.240707523384267930, 5.000000000000000000 ) ) ;
#105935=EDGE_CURVE ( 'NONE', #17123, #60821, #88137, .T. ) ;
#105936=ORIENTED_EDGE ( 'NONE', *, *, #89496, .F. ) ;
#105937=CARTESIAN_POINT ( 'NONE',  ( 0.1839886062690032631, 28.73617430169787568, 5.000000000000000000 ) ) ;
#105938=EDGE_LOOP ( 'NONE', ( #61650, #8651, #130124, #69006 ) ) ;
#105939=FACE_OUTER_BOUND ( 'NONE', #5797, .T. ) ;
#105940=CARTESIAN_POINT ( 'NONE',  ( -1.499999999999990896, -20.56887692260760048, 4.000000000000000000 ) ) ;
#105941=CARTESIAN_POINT ( 'NONE',  ( -33.41161490594808470, 22.22500000000000497, 4.777194822843813249 ) ) ;
#105944=ADVANCED_FACE ( 'NONE', ( #11294 ), #33136, .F. ) ;
#105946=ORIENTED_EDGE ( 'NONE', *, *, #62356, .T. ) ;
#105947=DIRECTION ( 'NONE',  ( -0.7071067811865486830, 0.7071067811865464625, 0.000000000000000000 ) ) ;
#105949=CARTESIAN_POINT ( 'NONE',  ( 31.49999999999977973, -10.53360074219763121, 5.000000000000000000 ) ) ;
#105950=DIRECTION ( 'NONE',  ( 0.000000000000000000, -1.000000000000000000, 0.000000000000000000 ) ) ;
#105951=VECTOR ( 'NONE', #26500, 1000.000000000000000 ) ;
#105952=DIRECTION ( 'NONE',  ( -0.7071067811865487940, 0.7071067811865463515, -0.000000000000000000 ) ) ;
#105954=ORIENTED_EDGE ( 'NONE', *, *, #120521, .F. ) ;
#105955=FACE_OUTER_BOUND ( 'NONE', #30611, .T. ) ;
#105956=DIRECTION ( 'NONE',  ( 0.7071067811865486830, -0.7071067811865464625, -0.000000000000000000 ) ) ;
#105957=ORIENTED_EDGE ( 'NONE', *, *, #77882, .T. ) ;
#105958=EDGE_LOOP ( 'NONE', ( #138889, #56573, #67600, #99009 ) ) ;
#105959=DIRECTION ( 'NONE',  ( -0.000000000000000000, 0.3543493200069153248, 0.9351131265310292928 ) ) ;
#105960=EDGE_LOOP ( 'NONE', ( #46010, #10271, #1551, #78140 ) ) ;
#105961=EDGE_CURVE ( 'NONE', #75676, #108628, #22188, .T. ) ;
#105962=DIRECTION ( 'NONE',  ( -0.7071067811865486830, -0.7071067811865464625, 0.000000000000000000 ) ) ;
#105964=CARTESIAN_POINT ( 'NONE',  ( -11.67183060077638856, 11.25929247661560595, 4.000000000000000000 ) ) ;
#105965=DIRECTION ( 'NONE',  ( -0.000000000000000000, -0.3543493200069152693, 0.9351131265310292928 ) ) ;
#105968=FACE_BOUND ( 'NONE', #93105, .T. ) ;
#105970=PLANE ( 'NONE',  #66469 ) ;
#105971=VERTEX_POINT ( 'NONE', #436 ) ;
#105972=DIRECTION ( 'NONE',  ( 0.3543493200069162685, -0.000000000000000000, -0.9351131265310288487 ) ) ;
#105973=CARTESIAN_POINT ( 'NONE',  ( -12.48921356237309155, -27.52281430457064104, 5.000000000000000000 ) ) ;
#105974=ORIENTED_EDGE ( 'NONE', *, *, #53086, .F. ) ;
#105975=ORIENTED_EDGE ( 'NONE', *, *, #70412, .T. ) ;
#105977=ORIENTED_EDGE ( 'NONE', *, *, #75314, .T. ) ;
#105978=EDGE_CURVE ( 'NONE', #95760, #135278, #44732, .T. ) ;
#105980=EDGE_LOOP ( 'NONE', ( #43814, #73974, #126464, #26997 ) ) ;
#105982=DIRECTION ( 'NONE',  ( -0.6830127018922180770, -0.6830127018922204085, -0.2588190451025213501 ) ) ;
#105985=ORIENTED_EDGE ( 'NONE', *, *, #134037, .T. ) ;
#105986=CARTESIAN_POINT ( 'NONE',  ( -51.48921356237309510, -27.52281430457091460, 5.000000000000000000 ) ) ;
#105987=EDGE_CURVE ( 'NONE', #92017, #110318, #45428, .T. ) ;
#105988=EDGE_CURVE ( 'NONE', #75431, #43122, #57016, .T. ) ;
#105990=LINE ( 'NONE', #137955, #64108 ) ;
#105991=CARTESIAN_POINT ( 'NONE',  ( 14.59122188827396549, 7.143407583703162089, 5.000000000000000000 ) ) ;
#105993=PLANE ( 'NONE',  #65478 ) ;
#105994=CARTESIAN_POINT ( 'NONE',  ( -30.48921356237309510, -27.52281430457076894, 5.000000000000000000 ) ) ;
#105995=ORIENTED_EDGE ( 'NONE', *, *, #65143, .F. ) ;
#105996=ORIENTED_EDGE ( 'NONE', *, *, #39665, .F. ) ;
#105997=CARTESIAN_POINT ( 'NONE',  ( 9.489213562373095101, -27.52281430457062328, 5.000000000000000000 ) ) ;
#105998=AXIS2_PLACEMENT_3D ( 'NONE', #80925, #36002, #23672 ) ;
#105999=CARTESIAN_POINT ( 'NONE',  ( -3.489213562373097322, -27.52281430457057709, 5.000000000000000000 ) ) ;
#106000=ORIENTED_EDGE ( 'NONE', *, *, #141757, .T. ) ;
#106001=ORIENTED_EDGE ( 'NONE', *, *, #52298, .T. ) ;
#106002=EDGE_LOOP ( 'NONE', ( #141884, #40476, #40885, #87548 ) ) ;
#106003=PLANE ( 'NONE',  #18912 ) ;
#106004=EDGE_CURVE ( 'NONE', #142848, #131756, #135287, .T. ) ;
#106006=DIRECTION ( 'NONE',  ( -0.000000000000000000, 0.000000000000000000, 1.000000000000000000 ) ) ;
#106008=DIRECTION ( 'NONE',  ( -0.000000000000000000, 0.000000000000000000, 1.000000000000000000 ) ) ;
#106009=VECTOR ( 'NONE', #103167, 1000.000000000000227 ) ;
#106010=VECTOR ( 'NONE', #124563, 1000.000000000000000 ) ;
#106011=EDGE_CURVE ( 'NONE', #139983, #24621, #24350, .T. ) ;
#106013=DIRECTION ( 'NONE',  ( -0.7071067811865486830, -0.7071067811865464625, 0.000000000000000000 ) ) ;
#106014=ORIENTED_EDGE ( 'NONE', *, *, #103694, .F. ) ;
#106015=CARTESIAN_POINT ( 'NONE',  ( 11.99999999999991651, -21.41253812416053748, 4.000000000000000000 ) ) ;
#106016=CARTESIAN_POINT ( 'NONE',  ( -51.18398860626899705, 28.73617430169823095, 5.000000000000000000 ) ) ;
#106017=FACE_OUTER_BOUND ( 'NONE', #6425, .T. ) ;
#106018=EDGE_CURVE ( 'NONE', #122980, #30015, #67154, .T. ) ;
#106019=LINE ( 'NONE', #50967, #100144 ) ;
#106020=ORIENTED_EDGE ( 'NONE', *, *, #139595, .T. ) ;
#106022=VERTEX_POINT ( 'NONE', #101191 ) ;
#106023=DIRECTION ( 'NONE',  ( -0.000000000000000000, -0.3543493200069152693, 0.9351131265310292928 ) ) ;
#106024=CARTESIAN_POINT ( 'NONE',  ( 66.18398860626901126, 28.73617430169833753, 5.000000000000000000 ) ) ;
#106026=ORIENTED_EDGE ( 'NONE', *, *, #5413, .T. ) ;
#106027=DIRECTION ( 'NONE',  ( 0.7071067811865487940, -0.7071067811865463515, 0.000000000000000000 ) ) ;
#106028=DIRECTION ( 'NONE',  ( 0.6830127018922181881, 0.6830127018922202975, -0.2588190451025214056 ) ) ;
#106029=DIRECTION ( 'NONE',  ( 0.7071067811865486830, -0.7071067811865464625, -0.000000000000000000 ) ) ;
#106031=ORIENTED_EDGE ( 'NONE', *, *, #12820, .T. ) ;
#106032=CARTESIAN_POINT ( 'NONE',  ( 7.734933297179447109, 12.75929247661558286, 18.34774599283954544 ) ) ;
#106033=CARTESIAN_POINT ( 'NONE',  ( -5.207106781186502609, -11.24070752338417201, 5.000000000000000000 ) ) ;
#106034=CARTESIAN_POINT ( 'NONE',  ( 42.18398860626899705, 28.73617430169816700, 5.000000000000000000 ) ) ;
#106035=CIRCLE ( 'NONE', #117620, 5.968999999999998529 ) ;
#106036=DIRECTION ( 'NONE',  ( -0.000000000000000000, 0.000000000000000000, 1.000000000000000000 ) ) ;
#106038=ORIENTED_EDGE ( 'NONE', *, *, #7755, .T. ) ;
#106039=ADVANCED_FACE ( 'NONE', ( #102646 ), #90316, .F. ) ;
#106040=VERTEX_POINT ( 'NONE', #22885 ) ;
#106041=VECTOR ( 'NONE', #1504, 1000.000000000000000 ) ;
#106042=EDGE_CURVE ( 'NONE', #140110, #57808, #14180, .T. ) ;
#106044=CARTESIAN_POINT ( 'NONE',  ( 42.18398860626899705, 28.73617430169816700, 5.000000000000000000 ) ) ;
#106045=EDGE_CURVE ( 'NONE', #110443, #24733, #100500, .T. ) ;
#106047=PLANE ( 'NONE',  #94465 ) ;
#106048=CARTESIAN_POINT ( 'NONE',  ( -28.17183060077627488, 6.759292476615645917, 4.000000000000000000 ) ) ;
#106050=EDGE_LOOP ( 'NONE', ( #48475, #108141, #120372, #97419 ) ) ;
#106051=FACE_OUTER_BOUND ( 'NONE', #53572, .T. ) ;
#106052=CARTESIAN_POINT ( 'NONE',  ( 34.92499999999999005, -6.281509562795680957, 4.759050581649329814 ) ) ;
#106053=DIRECTION ( 'NONE',  ( 0.6830127018922181881, 0.6830127018922202975, -0.2588190451025214056 ) ) ;
#106054=AXIS2_PLACEMENT_3D ( 'NONE', #79701, #91936, #36154 ) ;
#106056=LINE ( 'NONE', #19078, #46504 ) ;
#106057=VECTOR ( 'NONE', #88814, 1000.000000000000000 ) ;
#106058=EDGE_LOOP ( 'NONE', ( #122666, #73611, #75455, #48552 ) ) ;
#106059=DIRECTION ( 'NONE',  ( 0.7071067811865487940, 0.7071067811865463515, -0.000000000000000000 ) ) ;
#106060=VERTEX_POINT ( 'NONE', #35264 ) ;
#106061=ADVANCED_FACE ( 'NONE', ( #114210 ), #1146, .T. ) ;
#106062=VERTEX_POINT ( 'NONE', #91741 ) ;
#106064=CARTESIAN_POINT ( 'NONE',  ( 0.000000000000000000, 0.000000000000000000, 5.000000000000000000 ) ) ;
#106065=CARTESIAN_POINT ( 'NONE',  ( 24.18398860626899705, 28.73617430169804265, 5.000000000000000000 ) ) ;
#106066=DIRECTION ( 'NONE',  ( -0.3543493200069162685, -0.000000000000000000, -0.9351131265310288487 ) ) ;
#106069=VERTEX_POINT ( 'NONE', #124381 ) ;
#106070=CARTESIAN_POINT ( 'NONE',  ( -13.99806943317891772, -22.22500000000000142, 4.500000000000000888 ) ) ;
#106071=CARTESIAN_POINT ( 'NONE',  ( 6.241694584251833433, 0.7592924766157138627, 14.37146558664981555 ) ) ;
#106072=CARTESIAN_POINT ( 'NONE',  ( -25.78678096696625843, 12.75929247661558996, 10.29404684609029275 ) ) ;
#106074=DIRECTION ( 'NONE',  ( -0.000000000000000000, -0.3543493200069152693, 0.9351131265310292928 ) ) ;
#106075=DIRECTION ( 'NONE',  ( 0.7071067811865486830, -0.7071067811865464625, -0.000000000000000000 ) ) ;
#106077=DIRECTION ( 'NONE',  ( 0.7071067811865487940, 0.7071067811865463515, 0.000000000000000000 ) ) ;
#106078=ORIENTED_EDGE ( 'NONE', *, *, #29839, .T. ) ;
#106080=AXIS2_PLACEMENT_3D ( 'NONE', #82168, #16881, #49540 ) ;
#106083=DIRECTION ( 'NONE',  ( -0.000000000000000000, 0.000000000000000000, 1.000000000000000000 ) ) ;
#106084=ADVANCED_FACE ( 'NONE', ( #25049 ), #79505, .F. ) ;
#106086=ORIENTED_EDGE ( 'NONE', *, *, #55829, .F. ) ;
#106091=ORIENTED_EDGE ( 'NONE', *, *, #107455, .F. ) ;
#106092=CARTESIAN_POINT ( 'NONE',  ( 12.32816939922344446, 8.259292476615637923, 4.000000000000000000 ) ) ;
#106093=ORIENTED_EDGE ( 'NONE', *, *, #34636, .F. ) ;
#106095=PLANE ( 'NONE',  #53928 ) ;
#106096=AXIS2_PLACEMENT_3D ( 'NONE', #66611, #102812, #35441 ) ;
#106098=LINE ( 'NONE', #118427, #1305 ) ;
#106099=LINE ( 'NONE', #31441, #90634 ) ;
#106100=VECTOR ( 'NONE', #82303, 999.9999999999998863 ) ;
#106101=CARTESIAN_POINT ( 'NONE',  ( 28.49999999999979039, 16.08746187583908949, 4.000000000000000000 ) ) ;
#106102=ADVANCED_FACE ( 'NONE', ( #28656 ), #70743, .T. ) ;
#106103=CARTESIAN_POINT ( 'NONE',  ( -21.29974487139158512, -27.71228299555221142, 4.000000000000000000 ) ) ;
#106104=AXIS2_PLACEMENT_3D ( 'NONE', #39773, #52056, #139802 ) ;
#106105=LINE ( 'NONE', #104708, #100843 ) ;
#106106=ORIENTED_EDGE ( 'NONE', *, *, #76406, .F. ) ;
#106107=EDGE_CURVE ( 'NONE', #38833, #126622, #82319, .T. ) ;
#106108=CARTESIAN_POINT ( 'NONE',  ( -29.99451991528749417, 28.92564299267958816, 4.000000000000000000 ) ) ;
#106109=CARTESIAN_POINT ( 'NONE',  ( -18.10180811604841011, 9.068207373850700748, 5.000000000000000000 ) ) ;
#106110=CARTESIAN_POINT ( 'NONE',  ( -10.49999999999992184, -16.91253812416058722, 4.000000000000000000 ) ) ;
#106113=CARTESIAN_POINT ( 'NONE',  ( -34.92500000000001137, 18.00612307739175222, 4.000000000000000000 ) ) ;
#106114=VECTOR ( 'NONE', #68494, 1000.000000000000000 ) ;
#106115=ORIENTED_EDGE ( 'NONE', *, *, #118068, .T. ) ;
#106116=VERTEX_POINT ( 'NONE', #62712 ) ;
#106118=CARTESIAN_POINT ( 'NONE',  ( -16.17183060077636014, 9.759292476615621936, 4.000000000000000000 ) ) ;
#106119=CARTESIAN_POINT ( 'NONE',  ( -17.99999999999986855, -13.44781430457069149, 5.000000000000000000 ) ) ;
#106120=CARTESIAN_POINT ( 'NONE',  ( 29.48334561358934991, 22.22500000000000142, 4.500000000000000888 ) ) ;
#106121=VERTEX_POINT ( 'NONE', #17726 ) ;
#106122=ORIENTED_EDGE ( 'NONE', *, *, #100448, .T. ) ;
#106123=VECTOR ( 'NONE', #34401, 1000.000000000000000 ) ;
#106124=DIRECTION ( 'NONE',  ( -0.7071067811865487940, 0.7071067811865463515, 0.000000000000000000 ) ) ;
#106125=CARTESIAN_POINT ( 'NONE',  ( -34.49999999999975131, 9.054329344830845727, 4.994342998332165884 ) ) ;
#106127=EDGE_CURVE ( 'NONE', #129488, #128836, #95310, .T. ) ;
#106128=VERTEX_POINT ( 'NONE', #59849 ) ;
#106131=ORIENTED_EDGE ( 'NONE', *, *, #50684, .F. ) ;
#106132=DIRECTION ( 'NONE',  ( -0.000000000000000000, 0.000000000000000000, 1.000000000000000000 ) ) ;
#106133=VECTOR ( 'NONE', #25256, 999.9999999999998863 ) ;
#106134=FACE_BOUND ( 'NONE', #137763, .T. ) ;
#106135=DIRECTION ( 'NONE',  ( 0.7071067811865486830, -0.7071067811865464625, -0.000000000000000000 ) ) ;
#106136=LINE ( 'NONE', #95291, #83697 ) ;
#106137=CARTESIAN_POINT ( 'NONE',  ( -34.42500000000001137, 16.54139925780184583, 5.000000000000000000 ) ) ;
#106139=ORIENTED_EDGE ( 'NONE', *, *, #44181, .T. ) ;
#106140=VECTOR ( 'NONE', #7101, 999.9999999999998863 ) ;
#106141=LINE ( 'NONE', #41628, #9273 ) ;
#106143=ORIENTED_EDGE ( 'NONE', *, *, #87087, .T. ) ;
#106144=EDGE_CURVE ( 'NONE', #58244, #92406, #83764, .T. ) ;
#106145=ORIENTED_EDGE ( 'NONE', *, *, #113857, .T. ) ;
#106147=ORIENTED_EDGE ( 'NONE', *, *, #3659, .F. ) ;
#106149=DIRECTION ( 'NONE',  ( 1.000000000000000000, -0.000000000000000000, -0.000000000000000000 ) ) ;
#106150=EDGE_CURVE ( 'NONE', #87892, #65237, #126500, .T. ) ;
#106151=PLANE ( 'NONE',  #141676 ) ;
#106153=CARTESIAN_POINT ( 'NONE',  ( -30.29974487139158867, -27.71228299555227537, 4.000000000000000000 ) ) ;
#106154=AXIS2_PLACEMENT_3D ( 'NONE', #84371, #138014, #6721 ) ;
#106155=EDGE_CURVE ( 'NONE', #11479, #79851, #106160, .T. ) ;
#106157=PLANE ( 'NONE',  #135082 ) ;
#106158=ORIENTED_EDGE ( 'NONE', *, *, #77569, .T. ) ;
#106159=CARTESIAN_POINT ( 'NONE',  ( -45.48921356237309510, -27.52281430457087197, 5.000000000000000000 ) ) ;
#106160=LINE ( 'NONE', #6831, #112636 ) ;
#106161=CARTESIAN_POINT ( 'NONE',  ( 9.183988606268997046, 28.73617430169793607, 5.000000000000000000 ) ) ;
#106162=CARTESIAN_POINT ( 'NONE',  ( -9.489213562373095101, -27.52281430457062328, 5.000000000000000000 ) ) ;
#106163=PLANE ( 'NONE',  #130340 ) ;
#106164=DIRECTION ( 'NONE',  ( -0.7071067811865486830, 0.7071067811865464625, 0.000000000000000000 ) ) ;
#106165=LINE ( 'NONE', #6128, #26061 ) ;
#106166=EDGE_LOOP ( 'NONE', ( #18770, #93302, #129714, #88835 ) ) ;
#106167=EDGE_CURVE ( 'NONE', #79985, #45274, #115588, .T. ) ;
#106168=DIRECTION ( 'NONE',  ( -0.7071067811865486830, -0.7071067811865464625, 0.000000000000000000 ) ) ;
#106169=LINE ( 'NONE', #128671, #92976 ) ;
#106170=VERTEX_POINT ( 'NONE', #117746 ) ;
#106171=ORIENTED_EDGE ( 'NONE', *, *, #64136, .T. ) ;
#106172=EDGE_CURVE ( 'NONE', #112546, #63574, #125822, .T. ) ;
#106176=ORIENTED_EDGE ( 'NONE', *, *, #659, .F. ) ;
#106177=ADVANCED_FACE ( 'NONE', ( #93178 ), #72188, .F. ) ;
#106182=DIRECTION ( 'NONE',  ( 0.6830127018922180770, -0.6830127018922204085, -0.2588190451025213501 ) ) ;
#106183=VERTEX_POINT ( 'NONE', #83024 ) ;
#106184=CARTESIAN_POINT ( 'NONE',  ( 36.48921356237310221, -27.52281430457080802, 5.000000000000000000 ) ) ;
#106185=FACE_OUTER_BOUND ( 'NONE', #143138, .T. ) ;
#106186=EDGE_CURVE ( 'NONE', #88846, #73668, #105456, .T. ) ;
#106187=CARTESIAN_POINT ( 'NONE',  ( -39.18398860626899705, 28.73617430169814568, 5.000000000000000000 ) ) ;
#106188=ORIENTED_EDGE ( 'NONE', *, *, #35678, .T. ) ;
#106190=DIRECTION ( 'NONE',  ( 0.6830127018922181881, 0.6830127018922202975, -0.2588190451025214056 ) ) ;
#106191=LINE ( 'NONE', #61345, #122518 ) ;
#106192=ORIENTED_EDGE ( 'NONE', *, *, #16642, .T. ) ;
#106193=FACE_OUTER_BOUND ( 'NONE', #59529, .T. ) ;
#106195=ORIENTED_EDGE ( 'NONE', *, *, #62369, .T. ) ;
#106196=ORIENTED_EDGE ( 'NONE', *, *, #16269, .T. ) ;
#106197=ORIENTED_EDGE ( 'NONE', *, *, #2999, .F. ) ;
#106198=FACE_OUTER_BOUND ( 'NONE', #107251, .T. ) ;
#106199=ADVANCED_FACE ( 'NONE', ( #98182 ), #96021, .F. ) ;
#106200=AXIS2_PLACEMENT_3D ( 'NONE', #117055, #91740, #17048 ) ;
#106201=VECTOR ( 'NONE', #20819, 1000.000000000000000 ) ;
#106202=AXIS2_PLACEMENT_3D ( 'NONE', #136300, #46500, #36981 ) ;
#106203=CARTESIAN_POINT ( 'NONE',  ( -6.328169399223484426, 11.25929247661560773, 4.000000000000000000 ) ) ;
#106204=CARTESIAN_POINT ( 'NONE',  ( -0.2997448713915885632, -27.71228299555206220, 4.000000000000000000 ) ) ;
#106205=CARTESIAN_POINT ( 'NONE',  ( 4.828169399223496860, -11.24070752338416845, 4.000000000000000000 ) ) ;
#106206=ORIENTED_EDGE ( 'NONE', *, *, #97627, .F. ) ;
#106207=FACE_OUTER_BOUND ( 'NONE', #84213, .T. ) ;
#106208=VERTEX_POINT ( 'NONE', #74296 ) ;
#106209=EDGE_CURVE ( 'NONE', #134021, #13302, #109759, .T. ) ;
#106210=VECTOR ( 'NONE', #98388, 999.9999999999998863 ) ;
#106212=EDGE_CURVE ( 'NONE', #137243, #2775, #53223, .T. ) ;
#106214=CARTESIAN_POINT ( 'NONE',  ( 8.206660635421465955, 21.75929247661549226, 4.998822639870702744 ) ) ;
#106217=DIRECTION ( 'NONE',  ( -0.7071067811865487940, 0.7071067811865463515, -0.000000000000000000 ) ) ;
#106218=VERTEX_POINT ( 'NONE', #132265 ) ;
#106219=VERTEX_POINT ( 'NONE', #130101 ) ;
#106220=ORIENTED_EDGE ( 'NONE', *, *, #17095, .T. ) ;
#106221=LINE ( 'NONE', #129422, #32504 ) ;
#106222=CARTESIAN_POINT ( 'NONE',  ( -13.79551713769220811, 6.008391563887172993, 4.335713449946893228 ) ) ;
#106223=PLANE ( 'NONE',  #114784 ) ;
#106224=VECTOR ( 'NONE', #39233, 999.9999999999998863 ) ;
#106225=DIRECTION ( 'NONE',  ( 1.000000000000000000, -0.000000000000000000, 0.000000000000000000 ) ) ;
#106227=CARTESIAN_POINT ( 'NONE',  ( -0.7928932188134494297, 18.75929247661552068, 5.000000000000000000 ) ) ;
#106229=VECTOR ( 'NONE', #24279, 1000.000000000000000 ) ;
#106230=CARTESIAN_POINT ( 'NONE',  ( -31.49999999999977973, -10.04351517176480257, -1.623559851933897624 ) ) ;
#106231=DIRECTION ( 'NONE',  ( 0.6830127018922180770, -0.6830127018922204085, -0.2588190451025213501 ) ) ;
#106233=FACE_OUTER_BOUND ( 'NONE', #38884, .T. ) ;
#106234=ORIENTED_EDGE ( 'NONE', *, *, #32611, .T. ) ;
#106235=CARTESIAN_POINT ( 'NONE',  ( 34.92499999999998295, -8.337538124160891684, 4.000000000000000000 ) ) ;
#106236=ORIENTED_EDGE ( 'NONE', *, *, #111123, .F. ) ;
#106237=VECTOR ( 'NONE', #114846, 1000.000000000000000 ) ;
#106238=AXIS2_PLACEMENT_3D ( 'NONE', #72816, #118387, #63351 ) ;
#106239=CARTESIAN_POINT ( 'NONE',  ( -39.18398860626899705, 28.73617430169814568, 5.000000000000000000 ) ) ;
#106241=ORIENTED_EDGE ( 'NONE', *, *, #70605, .F. ) ;
#106242=DIRECTION ( 'NONE',  ( 1.000000000000000000, 0.000000000000000000, 0.000000000000000000 ) ) ;
#106243=DIRECTION ( 'NONE',  ( -0.7071067811865486830, -0.7071067811865463515, 0.000000000000000000 ) ) ;
#106244=EDGE_LOOP ( 'NONE', ( #62138, #83345, #64524, #9359 ) ) ;
#106245=ORIENTED_EDGE ( 'NONE', *, *, #101647, .F. ) ;
#106246=DIRECTION ( 'NONE',  ( 0.7071067811865487940, 0.7071067811865463515, -0.000000000000000000 ) ) ;
#106247=CARTESIAN_POINT ( 'NONE',  ( -21.18398860626899349, 28.73617430169802134, 5.000000000000000000 ) ) ;
#106248=VECTOR ( 'NONE', #12127, 1000.000000000000000 ) ;
#106252=LINE ( 'NONE', #6925, #83383 ) ;
#106254=ORIENTED_EDGE ( 'NONE', *, *, #95577, .T. ) ;
#106255=FACE_OUTER_BOUND ( 'NONE', #99047, .T. ) ;
#106259=FACE_OUTER_BOUND ( 'NONE', #45820, .T. ) ;
#106260=EDGE_LOOP ( 'NONE', ( #102115, #57959, #61186, #123996 ) ) ;
#106261=CARTESIAN_POINT ( 'NONE',  ( 22.37177410554622980, -1.784312229707115893, 4.000000000000000000 ) ) ;
#106262=EDGE_CURVE ( 'NONE', #90802, #98883, #64126, .T. ) ;
#106265=PLANE ( 'NONE',  #43200 ) ;
#106266=DIRECTION ( 'NONE',  ( 0.3543493200069162685, -0.000000000000000000, -0.9351131265310288487 ) ) ;
#106267=LINE ( 'NONE', #139686, #45644 ) ;
#106268=ORIENTED_EDGE ( 'NONE', *, *, #44984, .T. ) ;
#106269=CARTESIAN_POINT ( 'NONE',  ( -14.99999999999987743, -16.44781430457066662, 5.000000000000000000 ) ) ;
#106271=CARTESIAN_POINT ( 'NONE',  ( -3.299744871391591339, -27.71228299555208352, 4.000000000000000000 ) ) ;
#106272=ADVANCED_FACE ( 'NONE', ( #119891 ), #107611, .F. ) ;
#106273=CARTESIAN_POINT ( 'NONE',  ( -19.05000000000000071, 3.174999999999997158, 4.000000000000000000 ) ) ;
#106274=ORIENTED_EDGE ( 'NONE', *, *, #92752, .F. ) ;
#106276=LINE ( 'NONE', #17846, #91666 ) ;
#106278=ADVANCED_FACE ( 'NONE', ( #19185 ), #30044, .F. ) ;
#106279=EDGE_CURVE ( 'NONE', #111687, #123393, #40944, .T. ) ;
#106280=EDGE_LOOP ( 'NONE', ( #100413, #56344, #102302, #68358 ) ) ;
#106281=ORIENTED_EDGE ( 'NONE', *, *, #36112, .T. ) ;
#106283=ORIENTED_EDGE ( 'NONE', *, *, #30792, .T. ) ;
#106284=EDGE_CURVE ( 'NONE', #89804, #133506, #98868, .T. ) ;
#106286=CARTESIAN_POINT ( 'NONE',  ( 24.64327148205084939, 5.259292476615662792, 4.831541298974423526 ) ) ;
#106287=PLANE ( 'NONE',  #50385 ) ;
#106288=VERTEX_POINT ( 'NONE', #109030 ) ;
#106289=PLANE ( 'NONE',  #44434 ) ;
#106291=EDGE_CURVE ( 'NONE', #123046, #33185, #43098, .T. ) ;
#106292=VERTEX_POINT ( 'NONE', #31496 ) ;
#106295=CARTESIAN_POINT ( 'NONE',  ( -7.499999999999942268, -7.912538124160680475, 4.000000000000000000 ) ) ;
#106297=EDGE_CURVE ( 'NONE', #20788, #8725, #129360, .T. ) ;
#106298=AXIS2_PLACEMENT_3D ( 'NONE', #13085, #23247, #25395 ) ;
#106299=VECTOR ( 'NONE', #63398, 999.9999999999998863 ) ;
#106300=( BOUNDED_CURVE ( )  B_SPLINE_CURVE ( 3, ( #68204, #112379, #2882, #48544 ),
 .UNSPECIFIED., .F., .F. ) 
 B_SPLINE_CURVE_WITH_KNOTS ( ( 4, 4 ),
 ( 1.901594255663624056, 1.933014472006547413 ),
 .UNSPECIFIED. ) 
 CURVE ( )  GEOMETRIC_REPRESENTATION_ITEM ( )  RATIONAL_B_SPLINE_CURVE ( ( 1.000000000000000000, 0.9999177325257868620, 0.9999177325257868620, 1.000000000000000000 ) ) 
 REPRESENTATION_ITEM ( '' )  );
#106301=ORIENTED_EDGE ( 'NONE', *, *, #98039, .T. ) ;
#106303=CIRCLE ( 'NONE', #76235, 5.968999999999998529 ) ;
#106304=CARTESIAN_POINT ( 'NONE',  ( -74.99451991528749772, 28.92564299267990435, 4.000000000000000000 ) ) ;
#106305=FACE_OUTER_BOUND ( 'NONE', #65241, .T. ) ;
#106306=CARTESIAN_POINT ( 'NONE',  ( 9.183988606268997046, 28.73617430169793607, 5.000000000000000000 ) ) ;
#106308=EDGE_CURVE ( 'NONE', #10836, #34731, #8963, .T. ) ;
#106310=CARTESIAN_POINT ( 'NONE',  ( 28.49999999999979750, -14.56887692260765732, 4.000000000000000000 ) ) ;
#106311=LINE ( 'NONE', #6988, #122945 ) ;
#106312=ORIENTED_EDGE ( 'NONE', *, *, #61249, .T. ) ;
#106314=VERTEX_POINT ( 'NONE', #30798 ) ;
#106315=ORIENTED_EDGE ( 'NONE', *, *, #47476, .F. ) ;
#106316=EDGE_CURVE ( 'NONE', #123911, #26035, #141692, .T. ) ;
#106317=VECTOR ( 'NONE', #10337, 1000.000000000000000 ) ;
#106318=AXIS2_PLACEMENT_3D ( 'NONE', #108333, #98227, #119236 ) ;
#106321=ADVANCED_FACE ( 'NONE', ( #88014 ), #87305, .F. ) ;
#106322=VECTOR ( 'NONE', #130751, 1000.000000000000227 ) ;
#106323=CARTESIAN_POINT ( 'NONE',  ( -34.49999999999975131, -20.56887692260760758, 4.000000000000000000 ) ) ;
#106324=VERTEX_POINT ( 'NONE', #35086 ) ;
#106325=PLANE ( 'NONE',  #108462 ) ;
#106326=CARTESIAN_POINT ( 'NONE',  ( 5.700255128608413102, -27.71228299555201957, 4.000000000000000000 ) ) ;
#106327=FACE_OUTER_BOUND ( 'NONE', #11257, .T. ) ;
#106328=LINE ( 'NONE', #28094, #80899 ) ;
#106329=VECTOR ( 'NONE', #41593, 1000.000000000000000 ) ;
#106331=ORIENTED_EDGE ( 'NONE', *, *, #131495, .T. ) ;
#106332=VECTOR ( 'NONE', #126263, 1000.000000000000227 ) ;
#106333=EDGE_CURVE ( 'NONE', #33900, #50012, #123528, .T. ) ;
#106334=DIRECTION ( 'NONE',  ( -0.000000000000000000, 0.3543493200069153248, 0.9351131265310292928 ) ) ;
#106335=CARTESIAN_POINT ( 'NONE',  ( -75.18398860626899705, 28.73617430169839793, 5.000000000000000000 ) ) ;
#106336=VECTOR ( 'NONE', #41008, 1000.000000000000000 ) ;
#106337=ORIENTED_EDGE ( 'NONE', *, *, #52904, .F. ) ;
#106338=PLANE ( 'NONE',  #50485 ) ;
#106339=VERTEX_POINT ( 'NONE', #111920 ) ;
#106340=ADVANCED_FACE ( 'NONE', ( #23460 ), #35809, .F. ) ;
#106341=CARTESIAN_POINT ( 'NONE',  ( 9.489213562373095101, -27.52281430457062328, 5.000000000000000000 ) ) ;
#106342=ORIENTED_EDGE ( 'NONE', *, *, #68660, .T. ) ;
#106346=VECTOR ( 'NONE', #108863, 1000.000000000000000 ) ;
#106347=CARTESIAN_POINT ( 'NONE',  ( -31.99806943317879515, -22.22500000000000142, 4.500000000000000888 ) ) ;
#106349=DIRECTION ( 'NONE',  ( -0.000000000000000000, -1.000000000000000000, -0.000000000000000000 ) ) ;
#106350=ADVANCED_FACE ( 'NONE', ( #11123 ), #135122, .F. ) ;
#106351=CARTESIAN_POINT ( 'NONE',  ( 45.18398860626900415, 28.73617430169818832, 5.000000000000000000 ) ) ;
#106352=VECTOR ( 'NONE', #24953, 1000.000000000000000 ) ;
#106354=ADVANCED_FACE ( 'NONE', ( #89433 ), #113312, .T. ) ;
#106355=CARTESIAN_POINT ( 'NONE',  ( 28.49999999999980460, 0.05218569542916537407, 5.000000000000000000 ) ) ;
#106356=DIRECTION ( 'NONE',  ( -0.000000000000000000, 0.3543493200069153248, 0.9351131265310291818 ) ) ;
#106358=DIRECTION ( 'NONE',  ( -0.000000000000000000, 0.000000000000000000, 1.000000000000000000 ) ) ;
#106359=VERTEX_POINT ( 'NONE', #46711 ) ;
#106360=ORIENTED_EDGE ( 'NONE', *, *, #66392, .T. ) ;
#106361=DIRECTION ( 'NONE',  ( -0.7071067811865486830, -0.7071067811865464625, 0.000000000000000000 ) ) ;
#106362=ORIENTED_EDGE ( 'NONE', *, *, #103262, .F. ) ;
#106363=PLANE ( 'NONE',  #125627 ) ;
#106364=DIRECTION ( 'NONE',  ( -0.7071067811865487940, 0.7071067811865463515, -0.000000000000000000 ) ) ;
#106365=LINE ( 'NONE', #60068, #81095 ) ;
#106366=DIRECTION ( 'NONE',  ( -0.3543493200069162685, -0.000000000000000000, -0.9351131265310288487 ) ) ;
#106367=ORIENTED_EDGE ( 'NONE', *, *, #81329, .F. ) ;
#106370=EDGE_CURVE ( 'NONE', #28133, #61121, #133667, .T. ) ;
#106372=CARTESIAN_POINT ( 'NONE',  ( 34.49999999999976552, -14.94567065516889848, 4.994342998332158778 ) ) ;
#106373=CARTESIAN_POINT ( 'NONE',  ( 13.82816939922344091, 12.75929247661558641, 4.000000000000000000 ) ) ;
#106374=LINE ( 'NONE', #62220, #69723 ) ;
#106375=ORIENTED_EDGE ( 'NONE', *, *, #131252, .T. ) ;
#106377=VERTEX_POINT ( 'NONE', #47418 ) ;
#106378=CARTESIAN_POINT ( 'NONE',  ( -12.51665438641036410, 22.22500000000000142, 4.500000000000000888 ) ) ;
#106380=DIRECTION ( 'NONE',  ( 0.7071067811865487940, 0.7071067811865463515, 0.000000000000000000 ) ) ;
#106383=DIRECTION ( 'NONE',  ( 0.7071067811865487940, 0.7071067811865463515, 0.000000000000000000 ) ) ;
#106384=DIRECTION ( 'NONE',  ( 0.6830127018922181881, 0.6830127018922202975, -0.2588190451025214056 ) ) ;
#106385=CARTESIAN_POINT ( 'NONE',  ( -22.11017322888195125, -22.22500000000000142, 4.785647885939353863 ) ) ;
#106388=LINE ( 'NONE', #138356, #30184 ) ;
#106389=VECTOR ( 'NONE', #71250, 1000.000000000000000 ) ;
#106390=VECTOR ( 'NONE', #13120, 1000.000000000000000 ) ;
#106391=VECTOR ( 'NONE', #112831, 1000.000000000000227 ) ;
#106393=DIRECTION ( 'NONE',  ( -0.6830127018922181881, 0.6830127018922202975, -0.2588190451025214056 ) ) ;
#106394=ORIENTED_EDGE ( 'NONE', *, *, #124080, .F. ) ;
#106396=CARTESIAN_POINT ( 'NONE',  ( -31.82816939922330945, -11.24070752338416490, 4.000000000000000000 ) ) ;
#106397=PLANE ( 'NONE',  #55745 ) ;
#106398=EDGE_LOOP ( 'NONE', ( #135706, #93714, #89643, #131228 ) ) ;
#106399=CARTESIAN_POINT ( 'NONE',  ( -13.49999999999990763, 8.900465351122141655, -2.516491619111481892 ) ) ;
#106400=DIRECTION ( 'NONE',  ( -0.3543493200069162685, -0.000000000000000000, -0.9351131265310288487 ) ) ;
#106401=ORIENTED_EDGE ( 'NONE', *, *, #143155, .T. ) ;
#106402=AXIS2_PLACEMENT_3D ( 'NONE', #95568, #92707, #39801 ) ;
#106403=ORIENTED_EDGE ( 'NONE', *, *, #84744, .T. ) ;
#106406=DIRECTION ( 'NONE',  ( 0.7071067811865487940, 0.7071067811865463515, 0.000000000000000000 ) ) ;
#106407=AXIS2_PLACEMENT_3D ( 'NONE', #108524, #107127, #86111 ) ;
#106408=CARTESIAN_POINT ( 'NONE',  ( -20.99451991528748707, 28.92564299267952777, 4.000000000000000000 ) ) ;
#106411=DIRECTION ( 'NONE',  ( 0.7071067811865487940, 0.7071067811865463515, 0.000000000000000000 ) ) ;
#106414=AXIS2_PLACEMENT_3D ( 'NONE', #13021, #90617, #55860 ) ;
#106415=DIRECTION ( 'NONE',  ( -0.3543493200069162685, -0.000000000000000000, -0.9351131265310288487 ) ) ;
#106416=VECTOR ( 'NONE', #100134, 1000.000000000000000 ) ;
#106417=DIRECTION ( 'NONE',  ( 0.6830127018922181881, 0.6830127018922202975, -0.2588190451025214056 ) ) ;
#106419=ORIENTED_EDGE ( 'NONE', *, *, #53395, .F. ) ;
#106422=VECTOR ( 'NONE', #40706, 1000.000000000000000 ) ;
#106423=CARTESIAN_POINT ( 'NONE',  ( 3.793339364578457662, 21.75929247661549937, 4.998822639870711626 ) ) ;
#106424=ORIENTED_EDGE ( 'NONE', *, *, #5463, .F. ) ;
#106426=LINE ( 'NONE', #107175, #97312 ) ;
#106427=CARTESIAN_POINT ( 'NONE',  ( 28.49999999999981171, -20.56887692260760048, 4.000000000000000000 ) ) ;
#106428=ORIENTED_EDGE ( 'NONE', *, *, #68920, .T. ) ;
#106429=VECTOR ( 'NONE', #86719, 1000.000000000000000 ) ;
#106430=LINE ( 'NONE', #28213, #20876 ) ;
#106431=VECTOR ( 'NONE', #97155, 999.9999999999998863 ) ;
#106432=CARTESIAN_POINT ( 'NONE',  ( 3.183988606268992161, 28.73617430169789699, 5.000000000000000000 ) ) ;
#106433=EDGE_CURVE ( 'NONE', #58071, #20334, #33658, .T. ) ;
#106435=CARTESIAN_POINT ( 'NONE',  ( 13.49999999999992006, -1.912538124160735542, 4.000000000000000000 ) ) ;
#106436=EDGE_CURVE ( 'NONE', #59940, #81437, #80727, .T. ) ;
#106437=EDGE_CURVE ( 'NONE', #43341, #91589, #68440, .T. ) ;
#106439=LINE ( 'NONE', #36082, #130515 ) ;
#106440=PLANE ( 'NONE',  #10387 ) ;
#106441=LINE ( 'NONE', #94869, #108150 ) ;
#106442=VECTOR ( 'NONE', #82258, 999.9999999999998863 ) ;
#106443=LINE ( 'NONE', #116642, #128619 ) ;
#106444=PLANE ( 'NONE',  #107221 ) ;
#106446=CARTESIAN_POINT ( 'NONE',  ( -36.48921356237310221, -27.52281430457080802, 5.000000000000000000 ) ) ;
#106447=DIRECTION ( 'NONE',  ( 0.7071067811865487940, -0.7071067811865463515, 0.000000000000000000 ) ) ;
#106448=EDGE_CURVE ( 'NONE', #143191, #117668, #25592, .T. ) ;
#106449=ADVANCED_FACE ( 'NONE', ( #100326 ), #2392, .F. ) ;
#106450=EDGE_LOOP ( 'NONE', ( #37769, #42604, #123473, #112318 ) ) ;
#106453=ORIENTED_EDGE ( 'NONE', *, *, #129559, .F. ) ;
#106454=EDGE_CURVE ( 'NONE', #129291, #112641, #63999, .T. ) ;
#106457=DIRECTION ( 'NONE',  ( 0.7071067811865487940, 0.7071067811865463515, 0.000000000000000000 ) ) ;
#106458=ORIENTED_EDGE ( 'NONE', *, *, #49699, .F. ) ;
#106459=LINE ( 'NONE', #7140, #113933 ) ;
#106460=FACE_OUTER_BOUND ( 'NONE', #68844, .T. ) ;
#106461=ADVANCED_FACE ( 'NONE', ( #67727 ), #122044, .F. ) ;
#106464=CARTESIAN_POINT ( 'NONE',  ( 5.999999999999967137, -16.06887692260765377, 4.000000000000000000 ) ) ;
#106467=DIRECTION ( 'NONE',  ( 0.6830127018922181881, 0.6830127018922202975, -0.2588190451025214056 ) ) ;
#106468=AXIS2_PLACEMENT_3D ( 'NONE', #70604, #124933, #59025 ) ;
#106469=DIRECTION ( 'NONE',  ( 0.3543493200069162685, -0.000000000000000000, -0.9351131265310288487 ) ) ;
#106470=VERTEX_POINT ( 'NONE', #36487 ) ;
#106471=VERTEX_POINT ( 'NONE', #22711 ) ;
#106473=CARTESIAN_POINT ( 'NONE',  ( -14.99999999999989519, 15.45873954670183537, -0.03131636524290794948 ) ) ;
#106474=CARTESIAN_POINT ( 'NONE',  ( 5.999999999999967137, 7.588810512006220144, -3.013526669885240761 ) ) ;
#106476=EDGE_CURVE ( 'NONE', #129269, #135619, #9317, .T. ) ;
#106477=AXIS2_PLACEMENT_3D ( 'NONE', #44812, #55649, #122291 ) ;
#106481=ORIENTED_EDGE ( 'NONE', *, *, #13486, .T. ) ;
#106482=EDGE_LOOP ( 'NONE', ( #128789, #135626, #128193, #87810 ) ) ;
#106486=ADVANCED_FACE ( 'NONE', ( #111164 ), #17566, .F. ) ;
#106488=VECTOR ( 'NONE', #91784, 1000.000000000000000 ) ;
#106489=DIRECTION ( 'NONE',  ( -0.7071067811865486830, -0.7071067811865464625, -0.000000000000000000 ) ) ;
#106490=LINE ( 'NONE', #60192, #26381 ) ;
#106491=ORIENTED_EDGE ( 'NONE', *, *, #38277, .F. ) ;
#106492=CARTESIAN_POINT ( 'NONE',  ( 5.510786437626906675, -27.52281430457051314, 5.000000000000000000 ) ) ;
#106494=VECTOR ( 'NONE', #53942, 999.9999999999998863 ) ;
#106495=DIRECTION ( 'NONE',  ( 1.000000000000000000, -0.000000000000000000, -0.000000000000000000 ) ) ;
#106496=FACE_OUTER_BOUND ( 'NONE', #38140, .T. ) ;
#106497=VECTOR ( 'NONE', #123574, 1000.000000000000000 ) ;
#106498=AXIS2_PLACEMENT_3D ( 'NONE', #61708, #85556, #84860 ) ;
#106500=EDGE_CURVE ( 'NONE', #69962, #68424, #93009, .T. ) ;
#106502=VERTEX_POINT ( 'NONE', #15405 ) ;
#106503=EDGE_CURVE ( 'NONE', #73610, #109637, #127797, .T. ) ;
#106504=VECTOR ( 'NONE', #4150, 1000.000000000000227 ) ;
#106505=CARTESIAN_POINT ( 'NONE',  ( -12.00548008471251293, 28.92564299267929684, 4.000000000000000000 ) ) ;
#106506=DIRECTION ( 'NONE',  ( -1.000000000000000000, 0.000000000000000000, -0.000000000000000000 ) ) ;
#106508=DIRECTION ( 'NONE',  ( -0.3543493200069162685, -0.000000000000000000, -0.9351131265310288487 ) ) ;
#106509=PLANE ( 'NONE',  #133787 ) ;
#106510=DIRECTION ( 'NONE',  ( -0.7071067811865487940, 0.7071067811865463515, -0.000000000000000000 ) ) ;
#106511=VERTEX_POINT ( 'NONE', #26332 ) ;
#106512=CARTESIAN_POINT ( 'NONE',  ( 16.49999999999988276, 10.94296225409028089, -9.576120664313215514 ) ) ;
#106513=EDGE_LOOP ( 'NONE', ( #77946, #38362, #121519, #28673 ) ) ;
#106514=VERTEX_POINT ( 'NONE', #71275 ) ;
#106515=AXIS2_PLACEMENT_3D ( 'NONE', #35180, #78664, #121437 ) ;
#106516=ADVANCED_FACE ( 'NONE', ( #139403 ), #28482, .F. ) ;
#106517=VERTEX_POINT ( 'NONE', #70587 ) ;
#106519=DIRECTION ( 'NONE',  ( 0.6830127018922180770, -0.6830127018922204085, -0.2588190451025213501 ) ) ;
#106520=FACE_OUTER_BOUND ( 'NONE', #88121, .T. ) ;
#106521=FACE_OUTER_BOUND ( 'NONE', #140165, .T. ) ;
#106523=ADVANCED_FACE ( 'NONE', ( #114733 ), #61830, .F. ) ;
#106524=CARTESIAN_POINT ( 'NONE',  ( -14.99999999999989342, -16.60178936734450161, 0.8616154019347151971 ) ) ;
#106525=CARTESIAN_POINT ( 'NONE',  ( -24.48921356237309510, -27.52281430457072631, 5.000000000000000000 ) ) ;
#106526=VECTOR ( 'NONE', #58749, 1000.000000000000114 ) ;
#106527=DIRECTION ( 'NONE',  ( -0.7071067811865487940, 0.7071067811865463515, -0.000000000000000000 ) ) ;
#106529=CARTESIAN_POINT ( 'NONE',  ( -7.828169399223471103, 6.759292476615647693, 4.000000000000000000 ) ) ;
#106530=AXIS2_PLACEMENT_3D ( 'NONE', #47245, #24009, #101546 ) ;
#106531=LINE ( 'NONE', #142763, #64437 ) ;
#106532=CARTESIAN_POINT ( 'NONE',  ( 12.18398860626900060, 28.73617430169795739, 5.000000000000000000 ) ) ;
#106533=VERTEX_POINT ( 'NONE', #48090 ) ;
#106535=ORIENTED_EDGE ( 'NONE', *, *, #73765, .T. ) ;
#106536=VERTEX_POINT ( 'NONE', #116186 ) ;
#106537=EDGE_LOOP ( 'NONE', ( #10767, #92235, #94656, #88079, #65466 ) ) ;
#106539=EDGE_LOOP ( 'NONE', ( #72890, #75170, #141525, #116327 ) ) ;
#106540=VECTOR ( 'NONE', #103226, 999.9999999999998863 ) ;
#106541=VERTEX_POINT ( 'NONE', #37936 ) ;
#106542=DIRECTION ( 'NONE',  ( 0.7071067811865487940, -0.7071067811865463515, 0.000000000000000000 ) ) ;
#106543=DIRECTION ( 'NONE',  ( -0.000000000000000000, -0.3543493200069152693, 0.9351131265310292928 ) ) ;
#106544=EDGE_CURVE ( 'NONE', #9752, #93361, #78826, .T. ) ;
#106545=AXIS2_PLACEMENT_3D ( 'NONE', #75088, #77235, #97501 ) ;
#106546=CARTESIAN_POINT ( 'NONE',  ( -11.99999999999991829, 10.55218569542905982, 5.000000000000000000 ) ) ;
#106547=VERTEX_POINT ( 'NONE', #61153 ) ;
#106548=DIRECTION ( 'NONE',  ( -0.6830127018922180770, -0.6830127018922204085, -0.2588190451025213501 ) ) ;
#106550=DIRECTION ( 'NONE',  ( -0.7071067811865487940, 0.7071067811865463515, 0.000000000000000000 ) ) ;
#106552=AXIS2_PLACEMENT_3D ( 'NONE', #13263, #133654, #23444 ) ;
#106556=CARTESIAN_POINT ( 'NONE',  ( -30.69326993309580587, -3.740707523384241728, 12.88036043432874678 ) ) ;
#106558=ORIENTED_EDGE ( 'NONE', *, *, #114729, .F. ) ;
#106561=VECTOR ( 'NONE', #2872, 1000.000000000000000 ) ;
#106562=ORIENTED_EDGE ( 'NONE', *, *, #38822, .F. ) ;
#106563=DIRECTION ( 'NONE',  ( -0.3543493200069163240, 0.000000000000000000, -0.9351131265310288487 ) ) ;
#106565=FACE_OUTER_BOUND ( 'NONE', #97971, .T. ) ;
#106566=DIRECTION ( 'NONE',  ( 0.7071067811865486830, -0.7071067811865464625, -0.000000000000000000 ) ) ;
#106568=EDGE_CURVE ( 'NONE', #14297, #2772, #105990, .T. ) ;
#106569=DIRECTION ( 'NONE',  ( -0.7071067811865486830, -0.7071067811865464625, 0.000000000000000000 ) ) ;
#106570=EDGE_CURVE ( 'NONE', #33281, #42329, #59687, .T. ) ;
#106571=DIRECTION ( 'NONE',  ( 0.7071067811865486830, -0.7071067811865464625, -0.000000000000000000 ) ) ;
#106572=LINE ( 'NONE', #140647, #88516 ) ;
#106573=ORIENTED_EDGE ( 'NONE', *, *, #95853, .F. ) ;
#106574=DIRECTION ( 'NONE',  ( -0.7071067811865486830, -0.7071067811865464625, -0.000000000000000000 ) ) ;
#106576=ORIENTED_EDGE ( 'NONE', *, *, #79095, .F. ) ;
#106578=ORIENTED_EDGE ( 'NONE', *, *, #14153, .T. ) ;
#106579=EDGE_CURVE ( 'NONE', #77379, #50386, #104593, .T. ) ;
#106580=DIRECTION ( 'NONE',  ( 1.000000000000000000, 0.000000000000000000, 0.000000000000000000 ) ) ;
#106581=CARTESIAN_POINT ( 'NONE',  ( -5.510786437626906675, -27.52281430457051314, 5.000000000000000000 ) ) ;
#106582=VECTOR ( 'NONE', #135036, 1000.000000000000000 ) ;
#106583=ORIENTED_EDGE ( 'NONE', *, *, #110263, .T. ) ;
#106584=CARTESIAN_POINT ( 'NONE',  ( 2.999999999999980016, -6.033600742197678279, 5.000000000000000000 ) ) ;
#106585=PLANE ( 'NONE',  #137825 ) ;
#106587=CARTESIAN_POINT ( 'NONE',  ( 0.4892135623730947680, -27.52281430457055578, 5.000000000000000000 ) ) ;
#106588=CARTESIAN_POINT ( 'NONE',  ( 21.48921356237309155, -27.52281430457070499, 5.000000000000000000 ) ) ;
#106589=LINE ( 'NONE', #75440, #111842 ) ;
#106590=DIRECTION ( 'NONE',  ( -0.7071067811865486830, -0.7071067811865464625, -0.000000000000000000 ) ) ;
#106591=CARTESIAN_POINT ( 'NONE',  ( 29.29289321881325137, -0.7407075233842770334, 5.000000000000000000 ) ) ;
#106592=LINE ( 'NONE', #51558, #90007 ) ;
#106593=VECTOR ( 'NONE', #142926, 1000.000000000000000 ) ;
#106594=DIRECTION ( 'NONE',  ( -0.000000000000000000, 0.3543493200069153248, 0.9351131265310292928 ) ) ;
#106595=LINE ( 'NONE', #94323, #40779 ) ;
#106596=ORIENTED_EDGE ( 'NONE', *, *, #13497, .F. ) ;
#106599=VECTOR ( 'NONE', #111532, 1000.000000000000000 ) ;
#106602=ORIENTED_EDGE ( 'NONE', *, *, #17022, .T. ) ;
#106603=VERTEX_POINT ( 'NONE', #82862 ) ;
#106604=ORIENTED_EDGE ( 'NONE', *, *, #57480, .T. ) ;
#106605=ADVANCED_FACE ( 'NONE', ( #50231 ), #42929, .F. ) ;
#106606=DIRECTION ( 'NONE',  ( 0.7071067811865487940, 0.7071067811865463515, -0.000000000000000000 ) ) ;
#106607=CARTESIAN_POINT ( 'NONE',  ( -12.48921356237309155, -27.52281430457064104, 5.000000000000000000 ) ) ;
#106608=VECTOR ( 'NONE', #122639, 1000.000000000000000 ) ;
#106609=VECTOR ( 'NONE', #62080, 1000.000000000000000 ) ;
#106610=VECTOR ( 'NONE', #30289, 1000.000000000000227 ) ;
#106612=VERTEX_POINT ( 'NONE', #64665 ) ;
#106615=CARTESIAN_POINT ( 'NONE',  ( -33.48921356237309510, -27.52281430457078670, 5.000000000000000000 ) ) ;
#106616=CARTESIAN_POINT ( 'NONE',  ( -36.18398860626899705, 28.73617430169812437, 5.000000000000000000 ) ) ;
#106617=CARTESIAN_POINT ( 'NONE',  ( 16.03163515922181404, 2.259292476615694323, 13.77329220150640765 ) ) ;
#106619=EDGE_LOOP ( 'NONE', ( #118242, #105312, #60931, #96190 ) ) ;
#106620=EDGE_CURVE ( 'NONE', #119532, #27906, #54520, .T. ) ;
#106622=FACE_OUTER_BOUND ( 'NONE', #114704, .T. ) ;
#106624=VECTOR ( 'NONE', #52786, 999.9999999999998863 ) ;
#106625=LINE ( 'NONE', #105913, #110659 ) ;
#106626=CARTESIAN_POINT ( 'NONE',  ( -29.99451991528749417, 28.92564299267958816, 4.000000000000000000 ) ) ;
#106627=DIRECTION ( 'NONE',  ( -0.7071067811865486830, 0.7071067811865464625, 0.000000000000000000 ) ) ;
#106629=DIRECTION ( 'NONE',  ( -0.7071067811865486830, -0.7071067811865464625, -0.000000000000000000 ) ) ;
#106630=EDGE_CURVE ( 'NONE', #34677, #97296, #98701, .T. ) ;
#106631=ADVANCED_FACE ( 'NONE', ( #20415 ), #43612, .F. ) ;
#106632=LINE ( 'NONE', #51587, #106422 ) ;
#106634=ORIENTED_EDGE ( 'NONE', *, *, #64932, .T. ) ;
#106637=VERTEX_POINT ( 'NONE', #21149 ) ;
#106638=CARTESIAN_POINT ( 'NONE',  ( 34.42499999999998295, 0.000000000000000000, 4.500000000000000888 ) ) ;
#106639=EDGE_CURVE ( 'NONE', #26708, #126797, #53807, .T. ) ;
#106640=VECTOR ( 'NONE', #90218, 999.9999999999998863 ) ;
#106642=EDGE_CURVE ( 'NONE', #79922, #137698, #120421, .T. ) ;
#106643=CARTESIAN_POINT ( 'NONE',  ( -19.05000000000000071, 3.174999999999997158, 5.000000000000000000 ) ) ;
#106644=LINE ( 'NONE', #105931, #141843 ) ;
#106646=DIRECTION ( 'NONE',  ( 0.7071067811865487940, 0.7071067811865463515, 0.000000000000000000 ) ) ;
#106647=VECTOR ( 'NONE', #33606, 999.9999999999998863 ) ;
#106648=EDGE_CURVE ( 'NONE', #93168, #45460, #75546, .T. ) ;
#106649=VECTOR ( 'NONE', #76381, 1000.000000000000000 ) ;
#106651=EDGE_LOOP ( 'NONE', ( #139514, #54348, #56158, #100933 ) ) ;
#106652=AXIS2_PLACEMENT_3D ( 'NONE', #20335, #99320, #76179 ) ;
#106653=CARTESIAN_POINT ( 'NONE',  ( 1.499999999999999556, 0.05218569542916363935, 5.000000000000000000 ) ) ;
#106654=EDGE_LOOP ( 'NONE', ( #22592, #7753, #96303, #112733 ) ) ;
#106655=LINE ( 'NONE', #83526, #52123 ) ;
#106656=VECTOR ( 'NONE', #136397, 1000.000000000000000 ) ;
#106657=FACE_OUTER_BOUND ( 'NONE', #73039, .T. ) ;
#106659=EDGE_CURVE ( 'NONE', #94040, #2296, #129184, .T. ) ;
#106660=DIRECTION ( 'NONE',  ( -0.000000000000000000, 0.000000000000000000, 1.000000000000000000 ) ) ;
#106664=ORIENTED_EDGE ( 'NONE', *, *, #30240, .F. ) ;
#106665=PLANE ( 'NONE',  #65596 ) ;
#106666=DIRECTION ( 'NONE',  ( 0.7071067811865486830, -0.7071067811865464625, -0.000000000000000000 ) ) ;
#106668=CARTESIAN_POINT ( 'NONE',  ( 5.671830600776435638, 20.25929247661551003, 4.000000000000000000 ) ) ;
#106669=ADVANCED_FACE ( 'NONE', ( #31328 ), #106706, .F. ) ;
#106672=CARTESIAN_POINT ( 'NONE',  ( 33.18398860626899705, 28.73617430169810305, 5.000000000000000000 ) ) ;
#106673=DIRECTION ( 'NONE',  ( -0.7071067811865486830, 0.7071067811865464625, 0.000000000000000000 ) ) ;
#106674=EDGE_LOOP ( 'NONE', ( #5453, #15150, #30108 ) ) ;
#106675=ORIENTED_EDGE ( 'NONE', *, *, #120213, .T. ) ;
#106676=AXIS2_PLACEMENT_3D ( 'NONE', #20878, #109332, #108573 ) ;
#106677=ORIENTED_EDGE ( 'NONE', *, *, #137864, .F. ) ;
#106679=VERTEX_POINT ( 'NONE', #140100 ) ;
#106681=ADVANCED_FACE ( 'NONE', ( #108843 ), #84983, .F. ) ;
#106682=VECTOR ( 'NONE', #12078, 1000.000000000000000 ) ;
#106684=FACE_BOUND ( 'NONE', #97456, .T. ) ;
#106685=LINE ( 'NONE', #7379, #59578 ) ;
#106687=CARTESIAN_POINT ( 'NONE',  ( 66.48921356237309510, -27.52281430457101763, 5.000000000000000000 ) ) ;
#106688=EDGE_LOOP ( 'NONE', ( #57012, #44189, #86822, #51070 ) ) ;
#106689=ORIENTED_EDGE ( 'NONE', *, *, #48611, .F. ) ;
#106692=CARTESIAN_POINT ( 'NONE',  ( -24.48921356237309510, -27.52281430457072631, 5.000000000000000000 ) ) ;
#106693=ADVANCED_FACE ( 'NONE', ( #87130 ), #74115, .F. ) ;
#106694=ORIENTED_EDGE ( 'NONE', *, *, #5241, .T. ) ;
#106696=ORIENTED_EDGE ( 'NONE', *, *, #52250, .T. ) ;
#106697=PLANE ( 'NONE',  #53377 ) ;
#106698=CARTESIAN_POINT ( 'NONE',  ( 65.99451991528749772, 28.92564299267984396, 4.000000000000000000 ) ) ;
#106699=EDGE_CURVE ( 'NONE', #108316, #75865, #85679, .T. ) ;
#106700=ORIENTED_EDGE ( 'NONE', *, *, #93518, .T. ) ;
#106701=DIRECTION ( 'NONE',  ( 0.7071067811865486830, -0.7071067811865464625, -0.000000000000000000 ) ) ;
#106702=VECTOR ( 'NONE', #25445, 1000.000000000000227 ) ;
#106703=( BOUNDED_CURVE ( )  B_SPLINE_CURVE ( 3, ( #81551, #93820, #125755, #26430 ),
 .UNSPECIFIED., .F., .F. ) 
 B_SPLINE_CURVE_WITH_KNOTS ( ( 4, 4 ),
 ( 3.953918675577642095, 4.014082184732835401 ),
 .UNSPECIFIED. ) 
 CURVE ( )  GEOMETRIC_REPRESENTATION_ITEM ( )  RATIONAL_B_SPLINE_CURVE ( ( 1.000000000000000000, 0.9996983854260930169, 0.9996983854260930169, 1.000000000000000000 ) ) 
 REPRESENTATION_ITEM ( '' )  );
#106704=AXIS2_PLACEMENT_3D ( 'NONE', #22897, #447, #12752 ) ;
#106706=PLANE ( 'NONE',  #135822 ) ;
#106707=EDGE_CURVE ( 'NONE', #17447, #99025, #109585, .T. ) ;
#106708=FACE_OUTER_BOUND ( 'NONE', #16106, .T. ) ;
#106709=CARTESIAN_POINT ( 'NONE',  ( -17.38161509397993854, -2.240707523384264377, 13.37739548510243459 ) ) ;
#106710=LINE ( 'NONE', #72745, #26123 ) ;
#106711=FACE_OUTER_BOUND ( 'NONE', #126428, .T. ) ;
#106713=VECTOR ( 'NONE', #36196, 1000.000000000000000 ) ;
#106714=AXIS2_PLACEMENT_3D ( 'NONE', #67815, #92347, #89516 ) ;
#106715=VECTOR ( 'NONE', #74359, 1000.000000000000000 ) ;
#106716=ORIENTED_EDGE ( 'NONE', *, *, #116968, .T. ) ;
#106717=AXIS2_PLACEMENT_3D ( 'NONE', #2897, #125412, #136994 ) ;
#106719=( BOUNDED_CURVE ( )  B_SPLINE_CURVE ( 3, ( #105057, #131642, #11976, #122156 ),
 .UNSPECIFIED., .F., .F. ) 
 B_SPLINE_CURVE_WITH_KNOTS ( ( 4, 4 ),
 ( 2.779374508378133601, 4.199602562396849592 ),
 .UNSPECIFIED. ) 
 CURVE ( )  GEOMETRIC_REPRESENTATION_ITEM ( )  RATIONAL_B_SPLINE_CURVE ( ( 1.000000000000000000, 0.8388583629366601624, 0.8388583629366601624, 1.000000000000000000 ) ) 
 REPRESENTATION_ITEM ( '' )  );
#106720=DIRECTION ( 'NONE',  ( -0.7071067811865486830, -0.7071067811865464625, -0.000000000000000000 ) ) ;
#106722=AXIS2_PLACEMENT_3D ( 'NONE', #98037, #132105, #142955 ) ;
#106723=ORIENTED_EDGE ( 'NONE', *, *, #94998, .F. ) ;
#106724=EDGE_LOOP ( 'NONE', ( #104532, #46475, #75616, #17551 ) ) ;
#106725=DIRECTION ( 'NONE',  ( -0.7071067811865486830, -0.7071067811865464625, 0.000000000000000000 ) ) ;
#106727=EDGE_CURVE ( 'NONE', #55207, #136089, #74855, .T. ) ;
#106728=CARTESIAN_POINT ( 'NONE',  ( 39.48921356237310221, -27.52281430457082934, 5.000000000000000000 ) ) ;
#106730=VECTOR ( 'NONE', #1947, 1000.000000000000000 ) ;
#106731=LINE ( 'NONE', #52366, #20810 ) ;
#106734=DIRECTION ( 'NONE',  ( -0.6830127018922180770, -0.6830127018922204085, -0.2588190451025213501 ) ) ;
#106735=ORIENTED_EDGE ( 'NONE', *, *, #38607, .F. ) ;
#106736=DIRECTION ( 'NONE',  ( 0.3543493200069162685, -0.000000000000000000, -0.9351131265310288487 ) ) ;
#106739=DIRECTION ( 'NONE',  ( 0.3543493200069162685, -0.000000000000000000, -0.9351131265310288487 ) ) ;
#106740=VECTOR ( 'NONE', #55473, 999.9999999999998863 ) ;
#106741=LINE ( 'NONE', #130686, #65843 ) ;
#106742=DIRECTION ( 'NONE',  ( -0.6830127018922181881, 0.6830127018922202975, -0.2588190451025214056 ) ) ;
#106743=ORIENTED_EDGE ( 'NONE', *, *, #135533, .F. ) ;
#106744=DIRECTION ( 'NONE',  ( 1.000000000000000000, 0.000000000000000000, 0.000000000000000000 ) ) ;
#106745=ORIENTED_EDGE ( 'NONE', *, *, #73311, .F. ) ;
#106748=ADVANCED_FACE ( 'NONE', ( #45095 ), #134211, .F. ) ;
#106749=FACE_OUTER_BOUND ( 'NONE', #11891, .T. ) ;
#106751=EDGE_CURVE ( 'NONE', #62473, #98546, #68275, .T. ) ;
#106753=CARTESIAN_POINT ( 'NONE',  ( 63.48921356237309510, -27.52281430457099631, 5.000000000000000000 ) ) ;
#106756=VECTOR ( 'NONE', #32579, 1000.000000000000000 ) ;
#106757=DIRECTION ( 'NONE',  ( 0.3543493200069162685, -0.000000000000000000, -0.9351131265310288487 ) ) ;
#106758=DIRECTION ( 'NONE',  ( -0.3543493200069162685, -0.000000000000000000, -0.9351131265310288487 ) ) ;
#106759=CARTESIAN_POINT ( 'NONE',  ( -34.42500000000001137, 20.97718569542920264, 5.000000000000000000 ) ) ;
#106760=EDGE_LOOP ( 'NONE', ( #44608, #106902, #42290, #85115, #5321 ) ) ;
#106761=DIRECTION ( 'NONE',  ( -0.7071067811865486830, 0.7071067811865464625, 0.000000000000000000 ) ) ;
#106763=CARTESIAN_POINT ( 'NONE',  ( 63.48921356237309510, -27.52281430457099631, 5.000000000000000000 ) ) ;
#106764=CARTESIAN_POINT ( 'NONE',  ( 0.7070132642930391231, -21.74070752338405654, 4.999753212805213565 ) ) ;
#106766=LINE ( 'NONE', #64714, #9073 ) ;
#106767=VERTEX_POINT ( 'NONE', #2213 ) ;
#106768=VECTOR ( 'NONE', #82062, 1000.000000000000000 ) ;
#106770=ORIENTED_EDGE ( 'NONE', *, *, #92911, .F. ) ;
#106771=DIRECTION ( 'NONE',  ( -0.6830127018922181881, 0.6830127018922202975, -0.2588190451025214056 ) ) ;
#106772=LINE ( 'NONE', #130713, #87632 ) ;
#106774=CARTESIAN_POINT ( 'NONE',  ( -2.999999999999975575, -21.41253812416053748, 4.000000000000000000 ) ) ;
#106775=AXIS2_PLACEMENT_3D ( 'NONE', #34983, #142314, #77763 ) ;
#106776=CARTESIAN_POINT ( 'NONE',  ( -34.92500000000001137, -11.99387692260794047, 4.000000000000000000 ) ) ;
#106777=DIRECTION ( 'NONE',  ( -0.6830127018922181881, 0.6830127018922202975, -0.2588190451025214056 ) ) ;
#106778=VERTEX_POINT ( 'NONE', #57376 ) ;
#106779=CARTESIAN_POINT ( 'NONE',  ( -30.48921356237309510, -27.52281430457076894, 5.000000000000000000 ) ) ;
#106780=DIRECTION ( 'NONE',  ( -0.3543493200069162685, -0.000000000000000000, -0.9351131265310288487 ) ) ;
#106781=VECTOR ( 'NONE', #64601, 1000.000000000000000 ) ;
#106784=PLANE ( 'NONE',  #76081 ) ;
#106786=CARTESIAN_POINT ( 'NONE',  ( -20.99451991528748707, 28.92564299267952777, 4.000000000000000000 ) ) ;
#106787=ORIENTED_EDGE ( 'NONE', *, *, #118147, .F. ) ;
#106788=PLANE ( 'NONE',  #11775 ) ;
#106789=ORIENTED_EDGE ( 'NONE', *, *, #142344, .F. ) ;
#106790=VECTOR ( 'NONE', #21623, 1000.000000000000000 ) ;
#106791=ORIENTED_EDGE ( 'NONE', *, *, #4720, .T. ) ;
#106794=CARTESIAN_POINT ( 'NONE',  ( 32.20710678118632586, 0.7592924766157052030, 5.000000000000000000 ) ) ;
#106795=DIRECTION ( 'NONE',  ( 0.3543493200069162685, -0.000000000000000000, -0.9351131265310288487 ) ) ;
#106796=LINE ( 'NONE', #17638, #4859 ) ;
#106797=CARTESIAN_POINT ( 'NONE',  ( 7.408325480989960354, -0.7407075233842770334, 14.76736230305382414 ) ) ;
#106798=DIRECTION ( 'NONE',  ( -0.7071067811865486830, -0.7071067811865464625, 0.000000000000000000 ) ) ;
#106799=ORIENTED_EDGE ( 'NONE', *, *, #142550, .T. ) ;
#106800=CARTESIAN_POINT ( 'NONE',  ( 21.48921356237309155, -27.52281430457070499, 5.000000000000000000 ) ) ;
#106801=DIRECTION ( 'NONE',  ( -0.7071067811865486830, -0.7071067811865464625, 0.000000000000000000 ) ) ;
#106802=DIRECTION ( 'NONE',  ( -0.7071067811865486830, -0.7071067811865464625, -0.000000000000000000 ) ) ;
#106805=FACE_OUTER_BOUND ( 'NONE', #94643, .T. ) ;
#106808=EDGE_CURVE ( 'NONE', #80619, #126257, #113136, .T. ) ;
#106809=CARTESIAN_POINT ( 'NONE',  ( 34.42499999999998295, 13.54139925780190445, 5.000000000000000000 ) ) ;
#106810=ORIENTED_EDGE ( 'NONE', *, *, #138477, .T. ) ;
#106811=ORIENTED_EDGE ( 'NONE', *, *, #59265, .F. ) ;
#106813=CARTESIAN_POINT ( 'NONE',  ( 0.000000000000000000, 0.000000000000000000, 5.000000000000000000 ) ) ;
#106814=EDGE_CURVE ( 'NONE', #16172, #44633, #10953, .T. ) ;
#106816=ADVANCED_FACE ( 'NONE', ( #76997 ), #32768, .T. ) ;
#106817=CARTESIAN_POINT ( 'NONE',  ( -8.207106781186480404, 6.759292476615647693, 5.000000000000000000 ) ) ;
#106818=ORIENTED_EDGE ( 'NONE', *, *, #11382, .T. ) ;
#106820=EDGE_CURVE ( 'NONE', #42487, #72813, #88575, .T. ) ;
#106821=CARTESIAN_POINT ( 'NONE',  ( 4.499999999999976019, 10.46639925780215208, 5.000000000000000000 ) ) ;
#106822=VECTOR ( 'NONE', #50239, 1000.000000000000000 ) ;
#106823=VECTOR ( 'NONE', #131506, 999.9999999999998863 ) ;
#106825=ORIENTED_EDGE ( 'NONE', *, *, #126637, .T. ) ;
#106826=CARTESIAN_POINT ( 'NONE',  ( -63.29974487139158867, -27.71228299555250274, 4.000000000000000000 ) ) ;
#106827=EDGE_LOOP ( 'NONE', ( #3935, #116599, #6339, #14884 ) ) ;
#106828=AXIS2_PLACEMENT_3D ( 'NONE', #115669, #26567, #113553 ) ;
#106829=VERTEX_POINT ( 'NONE', #13812 ) ;
#106830=AXIS2_PLACEMENT_3D ( 'NONE', #90424, #3390, #123793 ) ;
#106831=VECTOR ( 'NONE', #57096, 1000.000000000000000 ) ;
#106833=DIRECTION ( 'NONE',  ( -1.000000000000000000, 0.000000000000000000, 0.000000000000000000 ) ) ;
#106834=AXIS2_PLACEMENT_3D ( 'NONE', #87692, #121027, #31187 ) ;
#106835=CARTESIAN_POINT ( 'NONE',  ( -0.7928932188134510950, 6.759292476615645917, 5.000000000000000000 ) ) ;
#106839=PLANE ( 'NONE',  #107706 ) ;
#106841=FACE_OUTER_BOUND ( 'NONE', #62631, .T. ) ;
#106842=CARTESIAN_POINT ( 'NONE',  ( -17.99999999999986855, -16.44781430457066662, 5.000000000000000000 ) ) ;
#106843=VERTEX_POINT ( 'NONE', #1506 ) ;
#106845=CARTESIAN_POINT ( 'NONE',  ( -5.999999999999963585, 14.58746187583910903, 4.000000000000000000 ) ) ;
#106847=CARTESIAN_POINT ( 'NONE',  ( 13.49999999999991473, 8.319652575858402344, -8.582050562765800805 ) ) ;
#106848=ADVANCED_FACE ( 'NONE', ( #66109 ), #110988, .F. ) ;
#106850=ORIENTED_EDGE ( 'NONE', *, *, #121383, .F. ) ;
#106851=AXIS2_PLACEMENT_3D ( 'NONE', #75713, #53979, #109753 ) ;
#106855=LINE ( 'NONE', #117025, #128809 ) ;
#106856=ORIENTED_EDGE ( 'NONE', *, *, #135884, .T. ) ;
#106857=EDGE_LOOP ( 'NONE', ( #55757, #33083, #39219, #64061 ) ) ;
#106858=EDGE_CURVE ( 'NONE', #129574, #141782, #93553, .T. ) ;
#106859=CARTESIAN_POINT ( 'NONE',  ( 30.70701326429282929, -21.74070752338406365, 4.999753212805224223 ) ) ;
#106860=ORIENTED_EDGE ( 'NONE', *, *, #80290, .F. ) ;
#106861=EDGE_LOOP ( 'NONE', ( #139054, #104270, #64261, #53498 ) ) ;
#106862=VECTOR ( 'NONE', #57698, 1000.000000000000227 ) ;
#106863=LINE ( 'NONE', #129331, #30522 ) ;
#106864=ORIENTED_EDGE ( 'NONE', *, *, #1926, .F. ) ;
#106865=AXIS2_PLACEMENT_3D ( 'NONE', #142258, #29184, #41481 ) ;
#106867=EDGE_CURVE ( 'NONE', #129881, #117528, #80553, .T. ) ;
#106870=FACE_BOUND ( 'NONE', #49730, .T. ) ;
#106871=DIRECTION ( 'NONE',  ( -0.7071067811865487940, 0.7071067811865463515, -0.000000000000000000 ) ) ;
#106874=DIRECTION ( 'NONE',  ( 0.3543493200069162685, -0.000000000000000000, -0.9351131265310288487 ) ) ;
#106876=ORIENTED_EDGE ( 'NONE', *, *, #10890, .T. ) ;
#106877=AXIS2_PLACEMENT_3D ( 'NONE', #98865, #45955, #1666 ) ;
#106880=ADVANCED_FACE ( 'NONE', ( #39173 ), #82683, .T. ) ;
#106881=VERTEX_POINT ( 'NONE', #5070 ) ;
#106882=VERTEX_POINT ( 'NONE', #59519 ) ;
#106884=ORIENTED_EDGE ( 'NONE', *, *, #8740, .F. ) ;
#106885=DIRECTION ( 'NONE',  ( 0.000000000000000000, -1.000000000000000000, 0.000000000000000000 ) ) ;
#106886=LINE ( 'NONE', #138831, #44293 ) ;
#106887=EDGE_CURVE ( 'NONE', #23670, #46353, #17403, .T. ) ;
#106888=AXIS2_PLACEMENT_3D ( 'NONE', #15187, #47879, #102241 ) ;
#106889=FACE_OUTER_BOUND ( 'NONE', #110354, .T. ) ;
#106890=VECTOR ( 'NONE', #74918, 1000.000000000000227 ) ;
#106891=FACE_OUTER_BOUND ( 'NONE', #110309, .T. ) ;
#106892=CARTESIAN_POINT ( 'NONE',  ( 34.49999999999975842, -11.94567065516892512, 4.994342998332160555 ) ) ;
#106894=ADVANCED_FACE ( 'NONE', ( #61660 ), #25415, .F. ) ;
#106897=CARTESIAN_POINT ( 'NONE',  ( -20.99999999999985789, -10.06887692260770883, 4.000000000000000000 ) ) ;
#106898=FACE_OUTER_BOUND ( 'NONE', #142898, .T. ) ;
#106899=PLANE ( 'NONE',  #101783 ) ;
#106900=AXIS2_PLACEMENT_3D ( 'NONE', #60454, #104631, #5297 ) ;
#106902=ORIENTED_EDGE ( 'NONE', *, *, #103996, .F. ) ;
#106903=CARTESIAN_POINT ( 'NONE',  ( 10.49999999999991829, 22.22500000000000142, 4.362957392718799454 ) ) ;
#106905=ORIENTED_EDGE ( 'NONE', *, *, #27801, .T. ) ;
#106906=ORIENTED_EDGE ( 'NONE', *, *, #43213, .F. ) ;
#106907=ADVANCED_FACE ( 'NONE', ( #92102 ), #28305, .F. ) ;
#106908=ORIENTED_EDGE ( 'NONE', *, *, #39718, .F. ) ;
#106910=VECTOR ( 'NONE', #67438, 1000.000000000000227 ) ;
#106913=( BOUNDED_CURVE ( )  B_SPLINE_CURVE ( 3, ( #87768, #88500, #10880, #90640 ),
 .UNSPECIFIED., .F., .T. ) 
 B_SPLINE_CURVE_WITH_KNOTS ( ( 4, 4 ),
 ( 2.001653308786165208, 3.503810798801449522 ),
 .UNSPECIFIED. ) 
 CURVE ( )  GEOMETRIC_REPRESENTATION_ITEM ( )  RATIONAL_B_SPLINE_CURVE ( ( 1.000000000000000000, 0.8206354192515235013, 0.8206354192515235013, 1.000000000000000000 ) ) 
 REPRESENTATION_ITEM ( '' )  );
#106916=VERTEX_POINT ( 'NONE', #14559 ) ;
#106918=CARTESIAN_POINT ( 'NONE',  ( -0.3301021854726499116, 17.25929247661554555, 19.83885114516071368 ) ) ;
#106920=CARTESIAN_POINT ( 'NONE',  ( 34.92499999999998295, -13.48753812416038933, 4.000000000000000000 ) ) ;
#106921=FACE_OUTER_BOUND ( 'NONE', #52550, .T. ) ;
#106922=VECTOR ( 'NONE', #126397, 1000.000000000000227 ) ;
#106924=DIRECTION ( 'NONE',  ( 0.6830127018922181881, 0.6830127018922202975, -0.2588190451025214056 ) ) ;
#106925=VERTEX_POINT ( 'NONE', #48622 ) ;
#106926=ORIENTED_EDGE ( 'NONE', *, *, #86039, .F. ) ;
#106928=AXIS2_PLACEMENT_3D ( 'NONE', #128168, #81093, #72390 ) ;
#106931=DIRECTION ( 'NONE',  ( 0.7071067811865487940, -0.7071067811865463515, 0.000000000000000000 ) ) ;
#106932=VERTEX_POINT ( 'NONE', #92824 ) ;
#106933=EDGE_CURVE ( 'NONE', #91285, #17335, #72565, .T. ) ;
#106934=VERTEX_POINT ( 'NONE', #15935 ) ;
#106935=ORIENTED_EDGE ( 'NONE', *, *, #104869, .T. ) ;
#106936=VERTEX_POINT ( 'NONE', #135635 ) ;
#106938=VECTOR ( 'NONE', #77278, 1000.000000000000000 ) ;
#106939=AXIS2_PLACEMENT_3D ( 'NONE', #67073, #23554, #65689 ) ;
#106941=LINE ( 'NONE', #115106, #72326 ) ;
#106942=CARTESIAN_POINT ( 'NONE',  ( -36.29974487139159578, -27.71228299555231445, 4.000000000000000000 ) ) ;
#106943=ADVANCED_FACE ( 'NONE', ( #104408 ), #49366, .F. ) ;
#106944=CARTESIAN_POINT ( 'NONE',  ( -34.92500000000001137, 15.75929247661555088, 4.255531930566231580 ) ) ;
#106946=ADVANCED_FACE ( 'NONE', ( #84135 ), #86256, .F. ) ;
#106947=CARTESIAN_POINT ( 'NONE',  ( -1.499999999999987566, -20.53675388469230612, 2.352720554255888885 ) ) ;
#106948=ORIENTED_EDGE ( 'NONE', *, *, #55659, .T. ) ;
#106949=CARTESIAN_POINT ( 'NONE',  ( 0.2997448713915885632, -27.71228299555206220, 4.000000000000000000 ) ) ;
#106951=DIRECTION ( 'NONE',  ( -0.7071067811865486830, -0.7071067811865464625, -0.000000000000000000 ) ) ;
#106952=VERTEX_POINT ( 'NONE', #96363 ) ;
#106953=CARTESIAN_POINT ( 'NONE',  ( -15.48921356237309510, -27.52281430457066236, 5.000000000000000000 ) ) ;
#106955=ORIENTED_EDGE ( 'NONE', *, *, #5857, .F. ) ;
#106956=VERTEX_POINT ( 'NONE', #30438 ) ;
#106957=DIRECTION ( 'NONE',  ( -0.7071067811865486830, -0.7071067811865464625, 0.000000000000000000 ) ) ;
#106958=CARTESIAN_POINT ( 'NONE',  ( 16.49999999999988631, -13.91253812416061564, 4.000000000000000000 ) ) ;
#106959=CARTESIAN_POINT ( 'NONE',  ( -32.99451991528749062, 28.92564299267960948, 4.000000000000000000 ) ) ;
#106960=DIRECTION ( 'NONE',  ( -0.7071067811865486830, -0.7071067811865464625, 0.000000000000000000 ) ) ;
#106962=EDGE_CURVE ( 'NONE', #139225, #88478, #20967, .T. ) ;
#106963=VECTOR ( 'NONE', #25775, 1000.000000000000000 ) ;
#106964=DIRECTION ( 'NONE',  ( 0.7071067811865487940, 0.7071067811865463515, -0.000000000000000000 ) ) ;
#106966=FACE_OUTER_BOUND ( 'NONE', #87453, .T. ) ;
#106967=LINE ( 'NONE', #87379, #120524 ) ;
#106969=VECTOR ( 'NONE', #102323, 1000.000000000000227 ) ;
#106970=ORIENTED_EDGE ( 'NONE', *, *, #130439, .F. ) ;
#106971=CARTESIAN_POINT ( 'NONE',  ( 0.000000000000000000, 0.000000000000000000, 5.000000000000000000 ) ) ;
#106972=ORIENTED_EDGE ( 'NONE', *, *, #47766, .T. ) ;
#106973=PLANE ( 'NONE',  #81782 ) ;
#106974=FACE_OUTER_BOUND ( 'NONE', #44056, .T. ) ;
#106975=AXIS2_PLACEMENT_3D ( 'NONE', #116820, #105232, #69793 ) ;
#106976=VERTEX_POINT ( 'NONE', #97831 ) ;
#106977=CARTESIAN_POINT ( 'NONE',  ( 34.92499999999998295, -10.48753812416042308, 4.000000000000000000 ) ) ;
#106978=ORIENTED_EDGE ( 'NONE', *, *, #73615, .F. ) ;
#106979=CARTESIAN_POINT ( 'NONE',  ( -19.05000000000000071, 3.174999999999997158, 1.444000000000000394 ) ) ;
#106980=LINE ( 'NONE', #75111, #88918 ) ;
#106981=ORIENTED_EDGE ( 'NONE', *, *, #116, .T. ) ;
#106982=EDGE_LOOP ( 'NONE', ( #100623, #125208, #107869, #24301 ) ) ;
#106983=CARTESIAN_POINT ( 'NONE',  ( 20.99999999999985079, 18.08204922493375122, 0.9627537363044395002 ) ) ;
#106984=CARTESIAN_POINT ( 'NONE',  ( 54.29974487139159578, -27.71228299555243879, 4.000000000000000000 ) ) ;
#106985=EDGE_CURVE ( 'NONE', #83429, #1085, #94952, .T. ) ;
#106986=VECTOR ( 'NONE', #135632, 999.9999999999998863 ) ;
#106989=CARTESIAN_POINT ( 'NONE',  ( 50.99451991528749062, 28.92564299267973738, 4.000000000000000000 ) ) ;
#106990=ADVANCED_FACE ( 'NONE', ( #52868 ), #119547, .F. ) ;
#106991=DIRECTION ( 'NONE',  ( -0.000000000000000000, -1.000000000000000000, -0.000000000000000000 ) ) ;
#106992=ORIENTED_EDGE ( 'NONE', *, *, #19840, .F. ) ;
#106994=EDGE_CURVE ( 'NONE', #44425, #122337, #8625, .T. ) ;
#106996=CARTESIAN_POINT ( 'NONE',  ( -2.163471288734491349, 15.75929247661555976, 9.299976744542915341 ) ) ;
#106997=AXIS2_PLACEMENT_3D ( 'NONE', #26631, #78899, #68051 ) ;
#106998=LINE ( 'NONE', #32125, #113917 ) ;
#106999=AXIS2_PLACEMENT_3D ( 'NONE', #139100, #41189, #20858 ) ;
#107000=ORIENTED_EDGE ( 'NONE', *, *, #24287, .F. ) ;
#107001=EDGE_CURVE ( 'NONE', #36869, #87685, #73938, .T. ) ;
#107002=EDGE_CURVE ( 'NONE', #53796, #114615, #108659, .T. ) ;
#107003=CARTESIAN_POINT ( 'NONE',  ( -32.99999999999976552, 7.552185695429097123, 5.000000000000000000 ) ) ;
#107004=ORIENTED_EDGE ( 'NONE', *, *, #38073, .F. ) ;
#107006=CARTESIAN_POINT ( 'NONE',  ( -34.92500000000001137, 22.22500000000000142, 4.000000000000000000 ) ) ;
#107007=LINE ( 'NONE', #107717, #49339 ) ;
#107008=AXIS2_PLACEMENT_3D ( 'NONE', #83441, #36365, #80594 ) ;
#107009=ORIENTED_EDGE ( 'NONE', *, *, #58413, .T. ) ;
#107010=DIRECTION ( 'NONE',  ( 0.7071067811865486830, -0.7071067811865464625, -0.000000000000000000 ) ) ;
#107011=FACE_OUTER_BOUND ( 'NONE', #88247, .T. ) ;
#107012=EDGE_CURVE ( 'NONE', #54435, #124219, #50760, .T. ) ;
#107013=CARTESIAN_POINT ( 'NONE',  ( 2.700255128608413990, -27.71228299555204089, 4.000000000000000000 ) ) ;
#107014=EDGE_CURVE ( 'NONE', #104818, #26316, #85499, .T. ) ;
#107015=LINE ( 'NONE', #140364, #38252 ) ;
#107016=EDGE_LOOP ( 'NONE', ( #20889, #112741, #75129, #27752 ) ) ;
#107017=DIRECTION ( 'NONE',  ( -0.7071067811865486830, -0.7071067811865464625, 0.000000000000000000 ) ) ;
#107018=CARTESIAN_POINT ( 'NONE',  ( -23.99999999999982947, -3.485240976185095096, -4.108735105802453269 ) ) ;
#107019=VECTOR ( 'NONE', #57472, 1000.000000000000000 ) ;
#107020=DIRECTION ( 'NONE',  ( 0.6830127018922180770, -0.6830127018922204085, -0.2588190451025213501 ) ) ;
#107022=ORIENTED_EDGE ( 'NONE', *, *, #28457, .F. ) ;
#107023=EDGE_LOOP ( 'NONE', ( #23053, #76645, #74353, #119168 ) ) ;
#107026=EDGE_CURVE ( 'NONE', #132815, #114242, #130479, .T. ) ;
#107027=DIRECTION ( 'NONE',  ( -0.7071067811865486830, 0.7071067811865464625, 0.000000000000000000 ) ) ;
#107029=CARTESIAN_POINT ( 'NONE',  ( 7.499999999999947597, -12.66682484999665625, -0.6294897503863775556 ) ) ;
#107030=CARTESIAN_POINT ( 'NONE',  ( 20.51078643762690490, -27.52281430457041012, 5.000000000000000000 ) ) ;
#107031=EDGE_LOOP ( 'NONE', ( #37592, #11285, #57785, #83762 ) ) ;
#107032=VECTOR ( 'NONE', #120481, 1000.000000000000000 ) ;
#107033=EDGE_CURVE ( 'NONE', #34652, #142342, #142074, .T. ) ;
#107035=VECTOR ( 'NONE', #102960, 1000.000000000000000 ) ;
#107037=LINE ( 'NONE', #71575, #113879 ) ;
#107038=VECTOR ( 'NONE', #19914, 1000.000000000000000 ) ;
#107039=VECTOR ( 'NONE', #128317, 999.9999999999998863 ) ;
#107040=VERTEX_POINT ( 'NONE', #31863 ) ;
#107042=AXIS2_PLACEMENT_3D ( 'NONE', #116833, #48738, #16810 ) ;
#107043=DIRECTION ( 'NONE',  ( 0.7071067811865486830, -0.7071067811865464625, -0.000000000000000000 ) ) ;
#107044=EDGE_CURVE ( 'NONE', #46544, #123966, #93639, .T. ) ;
#107045=CARTESIAN_POINT ( 'NONE',  ( 19.69064382391260892, -2.759520746520534473, 4.000000000000000000 ) ) ;
#107048=VERTEX_POINT ( 'NONE', #106529 ) ;
#107049=ORIENTED_EDGE ( 'NONE', *, *, #22386, .T. ) ;
#107050=DIRECTION ( 'NONE',  ( 0.7071067811865487940, 0.7071067811865463515, 0.000000000000000000 ) ) ;
#107051=CARTESIAN_POINT ( 'NONE',  ( -50.99451991528749062, 28.92564299267973738, 4.000000000000000000 ) ) ;
#107052=PLANE ( 'NONE',  #108665 ) ;
#107053=EDGE_CURVE ( 'NONE', #8350, #126973, #7213, .T. ) ;
#107054=CARTESIAN_POINT ( 'NONE',  ( 5.700255128608413102, -27.71228299555201957, 4.000000000000000000 ) ) ;
#107055=CARTESIAN_POINT ( 'NONE',  ( -17.99999999999986855, -6.412538124160685804, 4.000000000000000000 ) ) ;
#107056=EDGE_CURVE ( 'NONE', #55424, #89048, #129734, .T. ) ;
#107061=EDGE_LOOP ( 'NONE', ( #42784, #8735, #126623, #45273 ) ) ;
#107062=ORIENTED_EDGE ( 'NONE', *, *, #27769, .F. ) ;
#107063=ORIENTED_EDGE ( 'NONE', *, *, #96349, .F. ) ;
#107064=ORIENTED_EDGE ( 'NONE', *, *, #62243, .F. ) ;
#107066=CARTESIAN_POINT ( 'NONE',  ( -17.99999999999987210, 10.93112307739206912, 4.000000000000000000 ) ) ;
#107068=ORIENTED_EDGE ( 'NONE', *, *, #90040, .F. ) ;
#107069=CARTESIAN_POINT ( 'NONE',  ( 19.49999999999986500, 15.43112307739202826, 4.000000000000000000 ) ) ;
#107070=CARTESIAN_POINT ( 'NONE',  ( 42.29974487139158157, -27.71228299555235708, 4.000000000000000000 ) ) ;
#107072=CARTESIAN_POINT ( 'NONE',  ( 4.001930566820951718, -22.22500000000000142, 4.500000000000000888 ) ) ;
#107073=DIRECTION ( 'NONE',  ( -1.000000000000000000, 0.000000000000000000, 0.000000000000000000 ) ) ;
#107074=VECTOR ( 'NONE', #66736, 1000.000000000000000 ) ;
#107075=CARTESIAN_POINT ( 'NONE',  ( -22.63753812416082667, 22.22500000000000142, 4.000000000000000000 ) ) ;
#107076=EDGE_LOOP ( 'NONE', ( #19711, #122864, #58227, #29775 ) ) ;
#107077=CARTESIAN_POINT ( 'NONE',  ( -78.18398860626899705, 28.73617430169841924, 5.000000000000000000 ) ) ;
#107078=PLANE ( 'NONE',  #74367 ) ;
#107079=ORIENTED_EDGE ( 'NONE', *, *, #31495, .F. ) ;
#107081=ORIENTED_EDGE ( 'NONE', *, *, #75753, .T. ) ;
#107082=DIRECTION ( 'NONE',  ( -0.7071067811865487940, 0.7071067811865463515, 0.000000000000000000 ) ) ;
#107083=ORIENTED_EDGE ( 'NONE', *, *, #32906, .T. ) ;
#107085=EDGE_LOOP ( 'NONE', ( #110166, #15130, #11475, #31696 ) ) ;
#107088=CARTESIAN_POINT ( 'NONE',  ( -23.99999999999984013, -8.151047557385094677, -8.977947279169748995 ) ) ;
#107090=CARTESIAN_POINT ( 'NONE',  ( -48.48921356237309510, -27.52281430457089328, 5.000000000000000000 ) ) ;
#107091=VECTOR ( 'NONE', #109182, 1000.000000000000227 ) ;
#107092=DIRECTION ( 'NONE',  ( -0.000000000000000000, 0.000000000000000000, 1.000000000000000000 ) ) ;
#107093=CARTESIAN_POINT ( 'NONE',  ( 30.29974487139158867, -27.71228299555227537, 4.000000000000000000 ) ) ;
#107094=LINE ( 'NONE', #127420, #110075 ) ;
#107095=VECTOR ( 'NONE', #102733, 1000.000000000000000 ) ;
#107096=DIRECTION ( 'NONE',  ( -0.7071067811865486830, 0.7071067811865464625, 0.000000000000000000 ) ) ;
#107097=DIRECTION ( 'NONE',  ( -0.7071067811865486830, -0.7071067811865464625, -0.000000000000000000 ) ) ;
#107098=DIRECTION ( 'NONE',  ( 0.6830127018922181881, 0.6830127018922202975, -0.2588190451025214056 ) ) ;
#107099=EDGE_LOOP ( 'NONE', ( #128266, #35939, #81258, #49742 ) ) ;
#107100=CARTESIAN_POINT ( 'NONE',  ( -7.499999999999944045, 16.18958161055402201, -11.56426086740813197 ) ) ;
#107101=ORIENTED_EDGE ( 'NONE', *, *, #132469, .F. ) ;
#107102=ORIENTED_EDGE ( 'NONE', *, *, #137481, .F. ) ;
#107104=VECTOR ( 'NONE', #140391, 1000.000000000000000 ) ;
#107105=ORIENTED_EDGE ( 'NONE', *, *, #99790, .F. ) ;
#107106=LINE ( 'NONE', #31009, #35197 ) ;
#107107=CARTESIAN_POINT ( 'NONE',  ( -23.99999999999982592, -9.033600742197648970, 5.000000000000000000 ) ) ;
#107108=ADVANCED_FACE ( 'NONE', ( #63095 ), #131170, .F. ) ;
#107110=ORIENTED_EDGE ( 'NONE', *, *, #95656, .T. ) ;
#107111=ADVANCED_FACE ( 'NONE', ( #140605 ), #10097, .F. ) ;
#107113=ORIENTED_EDGE ( 'NONE', *, *, #113061, .F. ) ;
#107115=DIRECTION ( 'NONE',  ( -0.7071067811865486830, -0.7071067811865464625, 0.000000000000000000 ) ) ;
#107116=CARTESIAN_POINT ( 'NONE',  ( 26.20710678118635784, -17.24070752338410628, 5.000000000000000000 ) ) ;
#107117=EDGE_CURVE ( 'NONE', #77708, #9606, #54363, .T. ) ;
#107118=CARTESIAN_POINT ( 'NONE',  ( 34.45011844616453800, 3.002304141593910014, 5.000000000000001776 ) ) ;
#107119=ORIENTED_EDGE ( 'NONE', *, *, #76077, .F. ) ;
#107124=VECTOR ( 'NONE', #12450, 1000.000000000000114 ) ;
#107125=DIRECTION ( 'NONE',  ( -0.7071067811865487940, 0.7071067811865463515, -0.000000000000000000 ) ) ;
#107127=DIRECTION ( 'NONE',  ( 0.6830127018922180770, -0.6830127018922204085, -0.2588190451025213501 ) ) ;
#107128=VECTOR ( 'NONE', #133530, 1000.000000000000227 ) ;
#107129=CARTESIAN_POINT ( 'NONE',  ( 34.75611968250419181, -13.29434930147582072, 4.955485411084880276 ) ) ;
#107131=DIRECTION ( 'NONE',  ( -0.7071067811865487940, 0.7071067811865463515, 0.000000000000000000 ) ) ;
#107132=VECTOR ( 'NONE', #84310, 1000.000000000000000 ) ;
#107133=FACE_OUTER_BOUND ( 'NONE', #99247, .T. ) ;
#107135=PLANE ( 'NONE',  #125383 ) ;
#107136=ORIENTED_EDGE ( 'NONE', *, *, #6266, .T. ) ;
#107137=LINE ( 'NONE', #63675, #46384 ) ;
#107138=VECTOR ( 'NONE', #67746, 1000.000000000000000 ) ;
#107140=EDGE_CURVE ( 'NONE', #140272, #1952, #21698, .T. ) ;
#107141=LINE ( 'NONE', #83264, #109525 ) ;
#107142=VERTEX_POINT ( 'NONE', #67364 ) ;
#107143=PLANE ( 'NONE',  #138682 ) ;
#107145=ORIENTED_EDGE ( 'NONE', *, *, #3658, .T. ) ;
#107146=CARTESIAN_POINT ( 'NONE',  ( 0.000000000000000000, -21.72500000000000142, 4.500000000000000888 ) ) ;
#107149=VERTEX_POINT ( 'NONE', #142762 ) ;
#107150=CARTESIAN_POINT ( 'NONE',  ( -9.183988606268997046, 28.73617430169793607, 5.000000000000000000 ) ) ;
#107152=ORIENTED_EDGE ( 'NONE', *, *, #130263, .T. ) ;
#107155=CARTESIAN_POINT ( 'NONE',  ( -26.67183060077628909, 14.25929247661557220, 4.000000000000000000 ) ) ;
#107156=VECTOR ( 'NONE', #70647, 1000.000000000000227 ) ;
#107157=DIRECTION ( 'NONE',  ( 0.3543493200069162685, -0.000000000000000000, -0.9351131265310288487 ) ) ;
#107159=ADVANCED_FACE ( 'NONE', ( #110111 ), #88403, .F. ) ;
#107163=DIRECTION ( 'NONE',  ( -0.6830127018922181881, 0.6830127018922202975, -0.2588190451025214056 ) ) ;
#107166=AXIS2_PLACEMENT_3D ( 'NONE', #22913, #86075, #121537 ) ;
#107168=ORIENTED_EDGE ( 'NONE', *, *, #107014, .F. ) ;
#107169=EDGE_CURVE ( 'NONE', #6884, #2746, #12939, .T. ) ;
#107170=ORIENTED_EDGE ( 'NONE', *, *, #108072, .F. ) ;
#107173=LINE ( 'NONE', #19459, #27135 ) ;
#107174=LINE ( 'NONE', #57831, #118008 ) ;
#107175=CARTESIAN_POINT ( 'NONE',  ( 27.65494483745365173, 5.259292476615662792, 12.77922209995900182 ) ) ;
#107177=EDGE_LOOP ( 'NONE', ( #88440, #2408, #72202, #71776 ) ) ;
#107179=CARTESIAN_POINT ( 'NONE',  ( -33.29974487139158867, -27.71228299555229313, 4.000000000000000000 ) ) ;
#107180=LINE ( 'NONE', #88312, #106624 ) ;
#107181=LINE ( 'NONE', #8539, #16451 ) ;
#107182=EDGE_CURVE ( 'NONE', #85826, #84933, #101393, .T. ) ;
#107185=CARTESIAN_POINT ( 'NONE',  ( -29.20710678118633652, 6.759292476615654799, 5.000000000000000000 ) ) ;
#107186=ORIENTED_EDGE ( 'NONE', *, *, #65947, .F. ) ;
#107188=CARTESIAN_POINT ( 'NONE',  ( 19.49999999999986500, 12.43112307739205491, 4.000000000000000000 ) ) ;
#107190=LINE ( 'NONE', #136981, #110380 ) ;
#107191=CARTESIAN_POINT ( 'NONE',  ( 2.700255128608413990, -27.71228299555204089, 4.000000000000000000 ) ) ;
#107193=VECTOR ( 'NONE', #29059, 1000.000000000000227 ) ;
#107194=ORIENTED_EDGE ( 'NONE', *, *, #103899, .T. ) ;
#107195=VERTEX_POINT ( 'NONE', #78235 ) ;
#107196=ORIENTED_EDGE ( 'NONE', *, *, #27761, .T. ) ;
#107198=ORIENTED_EDGE ( 'NONE', *, *, #1238, .T. ) ;
#107199=EDGE_CURVE ( 'NONE', #115184, #4136, #122420, .T. ) ;
#107200=AXIS2_PLACEMENT_3D ( 'NONE', #48972, #16287, #91736 ) ;
#107202=VECTOR ( 'NONE', #43022, 1000.000000000000000 ) ;
#107203=CARTESIAN_POINT ( 'NONE',  ( -12.32816939922343913, -12.74070752338415602, 4.000000000000000000 ) ) ;
#107204=ORIENTED_EDGE ( 'NONE', *, *, #90049, .F. ) ;
#107205=EDGE_CURVE ( 'NONE', #91285, #51446, #49186, .T. ) ;
#107206=DIRECTION ( 'NONE',  ( -0.6830127018922181881, 0.6830127018922202975, -0.2588190451025214056 ) ) ;
#107207=CARTESIAN_POINT ( 'NONE',  ( 4.226741607178313487, -11.24070752338416135, 18.24660765846983068 ) ) ;
#107209=ORIENTED_EDGE ( 'NONE', *, *, #86853, .T. ) ;
#107210=DIRECTION ( 'NONE',  ( 0.7071067811865486830, -0.7071067811865464625, -0.000000000000000000 ) ) ;
#107211=ORIENTED_EDGE ( 'NONE', *, *, #44794, .F. ) ;
#107212=LINE ( 'NONE', #107898, #61557 ) ;
#107213=CARTESIAN_POINT ( 'NONE',  ( 22.49999999999984723, 13.46639925780212721, 5.000000000000000000 ) ) ;
#107214=CARTESIAN_POINT ( 'NONE',  ( 6.005480084712508493, 28.92564299267933947, 4.000000000000000000 ) ) ;
#107215=ORIENTED_EDGE ( 'NONE', *, *, #128450, .T. ) ;
#107216=VERTEX_POINT ( 'NONE', #93379 ) ;
#107217=VERTEX_POINT ( 'NONE', #38293 ) ;
#107218=CARTESIAN_POINT ( 'NONE',  ( 23.99451991528749062, 28.92564299267954908, 4.000000000000000000 ) ) ;
#107219=FACE_OUTER_BOUND ( 'NONE', #116102, .T. ) ;
#107221=AXIS2_PLACEMENT_3D ( 'NONE', #29618, #94872, #95601 ) ;
#107223=EDGE_CURVE ( 'NONE', #43460, #127258, #36847, .T. ) ;
#107224=( LENGTH_UNIT ( ) NAMED_UNIT ( * ) SI_UNIT ( .MILLI., .METRE. ) );
#107225=EDGE_CURVE ( 'NONE', #38928, #103858, #24200, .T. ) ;
#107226=EDGE_LOOP ( 'NONE', ( #131155, #66928, #101102, #34713 ) ) ;
#107228=LINE ( 'NONE', #17369, #85033 ) ;
#107229=ORIENTED_EDGE ( 'NONE', *, *, #139089, .T. ) ;
#107230=ORIENTED_EDGE ( 'NONE', *, *, #113248, .F. ) ;
#107231=VECTOR ( 'NONE', #15803, 1000.000000000000227 ) ;
#107232=VECTOR ( 'NONE', #125478, 999.9999999999998863 ) ;
#107234=LINE ( 'NONE', #27524, #130490 ) ;
#107236=CARTESIAN_POINT ( 'NONE',  ( -60.18398860626900415, 28.73617430169829490, 5.000000000000000000 ) ) ;
#107238=CARTESIAN_POINT ( 'NONE',  ( -3.084913231937595590, -12.74070752338414891, 18.74364270924353448 ) ) ;
#107241=PLANE ( 'NONE',  #85416 ) ;
#107242=EDGE_LOOP ( 'NONE', ( #26203, #118202, #142551, #121750 ) ) ;
#107244=CARTESIAN_POINT ( 'NONE',  ( 25.00442415654155681, 3.591886032380943838, 4.000000000000000000 ) ) ;
#107245=ORIENTED_EDGE ( 'NONE', *, *, #46240, .F. ) ;
#107246=LINE ( 'NONE', #63773, #15617 ) ;
#107249=ORIENTED_EDGE ( 'NONE', *, *, #42576, .T. ) ;
#107250=CARTESIAN_POINT ( 'NONE',  ( -33.48921356237309510, -27.52281430457078670, 5.000000000000000000 ) ) ;
#107251=EDGE_LOOP ( 'NONE', ( #7673, #36632, #52758, #29555 ) ) ;
#107252=ORIENTED_EDGE ( 'NONE', *, *, #86407, .T. ) ;
#107253=EDGE_LOOP ( 'NONE', ( #128155, #15160, #38848, #30637 ) ) ;
#107255=CIRCLE ( 'NONE', #30821, 5.968999999999998529 ) ;
#107256=LINE ( 'NONE', #42756, #71530 ) ;
#107257=DIRECTION ( 'NONE',  ( -0.7071067811865486830, -0.7071067811865464625, 0.000000000000000000 ) ) ;
#107258=CARTESIAN_POINT ( 'NONE',  ( -7.499999999999947597, 8.900465351122141655, -2.516491619111497435 ) ) ;
#107259=CARTESIAN_POINT ( 'NONE',  ( 10.22674160717827085, -11.24070752338416845, 18.24660765846984845 ) ) ;
#107260=EDGE_CURVE ( 'NONE', #35412, #109145, #39000, .T. ) ;
#107261=DIRECTION ( 'NONE',  ( 0.6830127018922180770, -0.6830127018922204085, -0.2588190451025213501 ) ) ;
#107262=CARTESIAN_POINT ( 'NONE',  ( -30.33229681110318410, 22.22500000000000142, 6.740346922533748675 ) ) ;
#107263=VECTOR ( 'NONE', #9749, 999.9999999999998863 ) ;
#107264=LINE ( 'NONE', #128335, #88574 ) ;
#107265=CARTESIAN_POINT ( 'NONE',  ( -30.48921356237309510, -27.52281430457076894, 5.000000000000000000 ) ) ;
#107266=PLANE ( 'NONE',  #89980 ) ;
#107267=VECTOR ( 'NONE', #32989, 999.9999999999998863 ) ;
#107268=FACE_OUTER_BOUND ( 'NONE', #19437, .T. ) ;
#107269=EDGE_LOOP ( 'NONE', ( #116442, #69949, #76136, #135444 ) ) ;
#107270=VERTEX_POINT ( 'NONE', #82510 ) ;
#107271=ORIENTED_EDGE ( 'NONE', *, *, #61697, .T. ) ;
#107272=VERTEX_POINT ( 'NONE', #92641 ) ;
#107274=ORIENTED_EDGE ( 'NONE', *, *, #28561, .T. ) ;
#107275=VECTOR ( 'NONE', #7616, 1000.000000000000000 ) ;
#107276=EDGE_CURVE ( 'NONE', #141475, #134787, #81094, .T. ) ;
#107277=ORIENTED_EDGE ( 'NONE', *, *, #121016, .F. ) ;
#107278=DIRECTION ( 'NONE',  ( 0.7071067811865487940, 0.7071067811865463515, -0.000000000000000000 ) ) ;
#107281=LINE ( 'NONE', #9365, #13783 ) ;
#107282=ORIENTED_EDGE ( 'NONE', *, *, #111719, .T. ) ;
#107284=ORIENTED_EDGE ( 'NONE', *, *, #141158, .F. ) ;
#107285=CARTESIAN_POINT ( 'NONE',  ( -15.72281430457048934, -21.72500000000000497, 5.000000000000000000 ) ) ;
#107286=VECTOR ( 'NONE', #96172, 1000.000000000000000 ) ;
#107287=EDGE_CURVE ( 'NONE', #58068, #41011, #15084, .T. ) ;
#107288=ADVANCED_FACE ( 'NONE', ( #2789 ), #115088, .F. ) ;
#107289=CARTESIAN_POINT ( 'NONE',  ( -11.29298673570688649, -21.74070752338406720, 4.999753212805217117 ) ) ;
#107290=VECTOR ( 'NONE', #17100, 1000.000000000000000 ) ;
#107292=VERTEX_POINT ( 'NONE', #27382 ) ;
#107294=LINE ( 'NONE', #36523, #11198 ) ;
#107296=DIRECTION ( 'NONE',  ( -0.7071067811865487940, 0.7071067811865463515, -0.000000000000000000 ) ) ;
#107298=ORIENTED_EDGE ( 'NONE', *, *, #118915, .T. ) ;
#107299=ORIENTED_EDGE ( 'NONE', *, *, #89475, .F. ) ;
#107301=EDGE_LOOP ( 'NONE', ( #91088, #68977, #41445 ) ) ;
#107302=CARTESIAN_POINT ( 'NONE',  ( 33.48921356237309510, -27.52281430457078670, 5.000000000000000000 ) ) ;
#107303=AXIS2_PLACEMENT_3D ( 'NONE', #296, #123575, #1708 ) ;
#107304=DIRECTION ( 'NONE',  ( -0.7071067811865487940, 0.7071067811865463515, -0.000000000000000000 ) ) ;
#107305=CARTESIAN_POINT ( 'NONE',  ( 36.18398860626899705, 28.73617430169812437, 5.000000000000000000 ) ) ;
#107306=DIRECTION ( 'NONE',  ( 0.7071067811865487940, 0.7071067811865463515, 0.000000000000000000 ) ) ;
#107307=ORIENTED_EDGE ( 'NONE', *, *, #41889, .F. ) ;
#107308=DIRECTION ( 'NONE',  ( 0.6830127018922180770, -0.6830127018922204085, -0.2588190451025213501 ) ) ;
#107310=DIRECTION ( 'NONE',  ( -0.7071067811865487940, 0.7071067811865463515, -0.000000000000000000 ) ) ;
#107312=ORIENTED_EDGE ( 'NONE', *, *, #59542, .F. ) ;
#107314=VECTOR ( 'NONE', #121381, 1000.000000000000000 ) ;
#107316=FACE_OUTER_BOUND ( 'NONE', #90499, .T. ) ;
#107318=LINE ( 'NONE', #118168, #44048 ) ;
#107320=ORIENTED_EDGE ( 'NONE', *, *, #129937, .F. ) ;
#107323=DIRECTION ( 'NONE',  ( -0.7071067811865487940, 0.7071067811865463515, -0.000000000000000000 ) ) ;
#107324=ADVANCED_FACE ( 'NONE', ( #117944 ), #140444, .F. ) ;
#107325=ORIENTED_EDGE ( 'NONE', *, *, #114159, .F. ) ;
#107326=LINE ( 'NONE', #119606, #81316 ) ;
#107328=CARTESIAN_POINT ( 'NONE',  ( 0.000000000000000000, 0.000000000000000000, 5.000000000000000000 ) ) ;
#107329=CARTESIAN_POINT ( 'NONE',  ( -31.49999999999978684, -20.53675388469233098, 2.352720554255818275 ) ) ;
#107330=VECTOR ( 'NONE', #64317, 1000.000000000000227 ) ;
#107331=CARTESIAN_POINT ( 'NONE',  ( 5.816011393731002066, 28.73617430169783304, 5.000000000000000000 ) ) ;
#107336=DIRECTION ( 'NONE',  ( -0.000000000000000000, 0.3543493200069153248, 0.9351131265310292928 ) ) ;
#107337=CARTESIAN_POINT ( 'NONE',  ( -81.18398860626899705, 28.73617430169844056, 5.000000000000000000 ) ) ;
#107338=DIRECTION ( 'NONE',  ( 1.000000000000000000, 0.000000000000000000, 0.000000000000000000 ) ) ;
#107339=FACE_OUTER_BOUND ( 'NONE', #136046, .T. ) ;
#107341=CARTESIAN_POINT ( 'NONE',  ( 30.18398860626900060, 28.73617430169808173, 5.000000000000000000 ) ) ;
#107342=ORIENTED_EDGE ( 'NONE', *, *, #132747, .F. ) ;
#107344=VERTEX_POINT ( 'NONE', #52712 ) ;
#107345=ORIENTED_EDGE ( 'NONE', *, *, #70258, .F. ) ;
#107346=EDGE_CURVE ( 'NONE', #29747, #62376, #40451, .T. ) ;
#107348=ORIENTED_EDGE ( 'NONE', *, *, #44468, .T. ) ;
#107349=ORIENTED_EDGE ( 'NONE', *, *, #119565, .F. ) ;
#107350=EDGE_CURVE ( 'NONE', #29747, #26803, #41861, .T. ) ;
#107351=EDGE_LOOP ( 'NONE', ( #131022, #55912, #36049, #142238 ) ) ;
#107353=PLANE ( 'NONE',  #90209 ) ;
#107355=CARTESIAN_POINT ( 'NONE',  ( -20.29289321881331176, -15.74070752338412049, 5.000000000000000000 ) ) ;
#107356=EDGE_CURVE ( 'NONE', #100536, #127633, #7774, .T. ) ;
#107357=DIRECTION ( 'NONE',  ( -1.000000000000000000, 0.000000000000000000, 0.000000000000000000 ) ) ;
#107358=LINE ( 'NONE', #8024, #141203 ) ;
#107359=DIRECTION ( 'NONE',  ( 0.6830127018922181881, 0.6830127018922202975, -0.2588190451025214056 ) ) ;
#107363=PLANE ( 'NONE',  #139581 ) ;
#107364=DIRECTION ( 'NONE',  ( -0.000000000000000000, 0.3543493200069153248, 0.9351131265310292928 ) ) ;
#107365=VECTOR ( 'NONE', #73063, 1000.000000000000227 ) ;
#107366=DIRECTION ( 'NONE',  ( 0.7071067811865487940, 0.7071067811865463515, 0.000000000000000000 ) ) ;
#107367=CARTESIAN_POINT ( 'NONE',  ( -30.48921356237309510, -27.52281430457076894, 5.000000000000000000 ) ) ;
#107368=DIRECTION ( 'NONE',  ( 0.7071067811865487940, 0.7071067811865463515, 0.000000000000000000 ) ) ;
#107369=CARTESIAN_POINT ( 'NONE',  ( 0.000000000000000000, 0.000000000000000000, 5.000000000000000000 ) ) ;
#107370=CARTESIAN_POINT ( 'NONE',  ( -36.18398860626899705, 28.73617430169812437, 5.000000000000000000 ) ) ;
#107372=ORIENTED_EDGE ( 'NONE', *, *, #31726, .T. ) ;
#107373=ORIENTED_EDGE ( 'NONE', *, *, #17298, .T. ) ;
#107375=ORIENTED_EDGE ( 'NONE', *, *, #13385, .T. ) ;
#107376=EDGE_CURVE ( 'NONE', #141174, #9436, #17242, .T. ) ;
#107377=DIRECTION ( 'NONE',  ( 0.6830127018922181881, 0.6830127018922202975, -0.2588190451025214056 ) ) ;
#107380=VECTOR ( 'NONE', #89992, 1000.000000000000000 ) ;
#107384=EDGE_CURVE ( 'NONE', #116374, #71694, #75224, .T. ) ;
#107385=AXIS2_PLACEMENT_3D ( 'NONE', #66845, #69000, #110312 ) ;
#107386=EDGE_LOOP ( 'NONE', ( #11446, #45106, #27219, #140634 ) ) ;
#107387=FACE_OUTER_BOUND ( 'NONE', #65305, .T. ) ;
#107388=VERTEX_POINT ( 'NONE', #94780 ) ;
#107389=FACE_OUTER_BOUND ( 'NONE', #121633, .T. ) ;
#107390=DIRECTION ( 'NONE',  ( -0.7071067811865487940, 0.7071067811865463515, 0.000000000000000000 ) ) ;
#107391=CARTESIAN_POINT ( 'NONE',  ( 2.999999999999984457, 16.55218569542899587, 5.000000000000000000 ) ) ;
#107392=VECTOR ( 'NONE', #128988, 999.9999999999998863 ) ;
#107393=FACE_OUTER_BOUND ( 'NONE', #129657, .T. ) ;
#107394=ORIENTED_EDGE ( 'NONE', *, *, #124220, .F. ) ;
#107396=ORIENTED_EDGE ( 'NONE', *, *, #113503, .F. ) ;
#107397=DIRECTION ( 'NONE',  ( 0.7071067811865487940, 0.7071067811865463515, 0.000000000000000000 ) ) ;
#107398=DIRECTION ( 'NONE',  ( -0.7071067811865487940, 0.7071067811865463515, 0.000000000000000000 ) ) ;
#107399=CARTESIAN_POINT ( 'NONE',  ( 23.99999999999984013, 8.966399257802171618, 5.000000000000000000 ) ) ;
#107401=VECTOR ( 'NONE', #23836, 999.9999999999998863 ) ;
#107402=ADVANCED_FACE ( 'NONE', ( #86078 ), #62922, .F. ) ;
#107403=AXIS2_PLACEMENT_3D ( 'NONE', #97072, #75382, #29703 ) ;
#107405=ORIENTED_EDGE ( 'NONE', *, *, #124911, .T. ) ;
#107406=DIRECTION ( 'NONE',  ( 0.7071067811865487940, 0.7071067811865463515, -0.000000000000000000 ) ) ;
#107407=ORIENTED_EDGE ( 'NONE', *, *, #56308, .T. ) ;
#107408=ORIENTED_EDGE ( 'NONE', *, *, #67957, .F. ) ;
#107410=ORIENTED_EDGE ( 'NONE', *, *, #17869, .F. ) ;
#107413=DIRECTION ( 'NONE',  ( -0.000000000000000000, 0.000000000000000000, 1.000000000000000000 ) ) ;
#107414=DIRECTION ( 'NONE',  ( -0.6830127018922181881, 0.6830127018922202975, -0.2588190451025214056 ) ) ;
#107415=ORIENTED_EDGE ( 'NONE', *, *, #64840, .F. ) ;
#107416=CARTESIAN_POINT ( 'NONE',  ( -18.29974487139159223, -27.71228299555219010, 4.000000000000000000 ) ) ;
#107417=LINE ( 'NONE', #138639, #105768 ) ;
#107419=LINE ( 'NONE', #42192, #38974 ) ;
#107421=FACE_BOUND ( 'NONE', #82755, .T. ) ;
#107422=ORIENTED_EDGE ( 'NONE', *, *, #52215, .F. ) ;
#107424=CARTESIAN_POINT ( 'NONE',  ( 22.49999999999985789, -11.94781430457070215, 5.000000000000000000 ) ) ;
#107425=DIRECTION ( 'NONE',  ( 0.6830127018922181881, 0.6830127018922202975, -0.2588190451025214056 ) ) ;
#107426=CARTESIAN_POINT ( 'NONE',  ( -31.49999999999977973, -2.947814304570804289, 5.000000000000000000 ) ) ;
#107427=ORIENTED_EDGE ( 'NONE', *, *, #69177, .F. ) ;
#107428=CARTESIAN_POINT ( 'NONE',  ( -34.92500000000001137, 5.831225763041756771, -1.212213889845635828 ) ) ;
#107430=ORIENTED_EDGE ( 'NONE', *, *, #72003, .T. ) ;
#107431=CARTESIAN_POINT ( 'NONE',  ( 3.813491353976365961, -15.74070752338412049, 8.904080028138931624 ) ) ;
#107432=EDGE_LOOP ( 'NONE', ( #101200, #10167, #139200 ) ) ;
#107434=VECTOR ( 'NONE', #121364, 1000.000000000000000 ) ;
#107435=ORIENTED_EDGE ( 'NONE', *, *, #25353, .F. ) ;
#107436=FACE_OUTER_BOUND ( 'NONE', #44766, .T. ) ;
#107437=CARTESIAN_POINT ( 'NONE',  ( -25.21498419724174767, -3.740707523384238176, 15.76143240460118200 ) ) ;
#107438=EDGE_LOOP ( 'NONE', ( #54578, #26406, #130279, #10660, #10924 ) ) ;
#107439=VECTOR ( 'NONE', #115420, 1000.000000000000227 ) ;
#107441=CARTESIAN_POINT ( 'NONE',  ( 32.27718569542918203, -21.72500000000000142, 5.000000000000000000 ) ) ;
#107442=DIRECTION ( 'NONE',  ( 0.7071067811865486830, -0.7071067811865463515, 0.000000000000000000 ) ) ;
#107443=CARTESIAN_POINT ( 'NONE',  ( 53.99451991528749062, 28.92564299267975869, 4.000000000000000000 ) ) ;
#107444=ORIENTED_EDGE ( 'NONE', *, *, #94149, .F. ) ;
#107445=VERTEX_POINT ( 'NONE', #107801 ) ;
#107446=CARTESIAN_POINT ( 'NONE',  ( -27.75860074219777118, 21.72500000000000142, 5.000000000000000000 ) ) ;
#107447=PLANE ( 'NONE',  #111495 ) ;
#107449=EDGE_CURVE ( 'NONE', #95865, #135641, #9173, .T. ) ;
#107450=EDGE_LOOP ( 'NONE', ( #4131, #102868, #102659, #20588 ) ) ;
#107452=CARTESIAN_POINT ( 'NONE',  ( 14.99999999999990230, 11.96639925780214320, 5.000000000000000000 ) ) ;
#107453=CARTESIAN_POINT ( 'NONE',  ( 63.18398860626900415, 28.73617430169831621, 5.000000000000000000 ) ) ;
#107454=ADVANCED_FACE ( 'NONE', ( #30256 ), #53439, .T. ) ;
#107455=EDGE_CURVE ( 'NONE', #71262, #102314, #46172, .T. ) ;
#107456=DIRECTION ( 'NONE',  ( -0.7071067811865487940, 0.7071067811865463515, -0.000000000000000000 ) ) ;
#107457=VERTEX_POINT ( 'NONE', #31695 ) ;
#107458=CARTESIAN_POINT ( 'NONE',  ( -5.671830600776425868, -15.74070752338412049, 4.000000000000000000 ) ) ;
#107460=CARTESIAN_POINT ( 'NONE',  ( 18.29974487139159223, -27.71228299555219010, 4.000000000000000000 ) ) ;
#107461=EDGE_CURVE ( 'NONE', #39522, #123360, #44762, .T. ) ;
#107462=EDGE_CURVE ( 'NONE', #9125, #138634, #90350, .T. ) ;
#107463=VECTOR ( 'NONE', #139496, 1000.000000000000000 ) ;
#107465=CARTESIAN_POINT ( 'NONE',  ( 8.999999999999932498, 5.966399257802197376, 5.000000000000000000 ) ) ;
#107466=EDGE_CURVE ( 'NONE', #134862, #10403, #12773, .T. ) ;
#107467=ORIENTED_EDGE ( 'NONE', *, *, #61472, .F. ) ;
#107470=EDGE_CURVE ( 'NONE', #130889, #99583, #44006, .T. ) ;
#107472=CARTESIAN_POINT ( 'NONE',  ( -34.92500000000001137, 18.85612307739224036, 4.000000000000000000 ) ) ;
#107473=LINE ( 'NONE', #19750, #14764 ) ;
#107474=ORIENTED_EDGE ( 'NONE', *, *, #42598, .T. ) ;
#107476=ORIENTED_EDGE ( 'NONE', *, *, #118390, .F. ) ;
#107477=ADVANCED_FACE ( 'NONE', ( #101221 ), #120085, .T. ) ;
#107479=DIRECTION ( 'NONE',  ( 0.3543493200069162685, -0.000000000000000000, -0.9351131265310288487 ) ) ;
#107481=VERTEX_POINT ( 'NONE', #56352 ) ;
#107482=EDGE_CURVE ( 'NONE', #358, #8173, #78069, .T. ) ;
#107483=CARTESIAN_POINT ( 'NONE',  ( 8.999999999999941380, 13.55218569542903140, 5.000000000000000000 ) ) ;
#107484=PLANE ( 'NONE',  #113558 ) ;
#107485=DIRECTION ( 'NONE',  ( -0.6830127018922181881, 0.6830127018922202975, -0.2588190451025214056 ) ) ;
#107486=VERTEX_POINT ( 'NONE', #143301 ) ;
#107487=LINE ( 'NONE', #30669, #134202 ) ;
#107489=ADVANCED_FACE ( 'NONE', ( #120826 ), #54199, .F. ) ;
#107491=DIRECTION ( 'NONE',  ( 0.3543493200069162685, -0.000000000000000000, -0.9351131265310288487 ) ) ;
#107492=AXIS2_PLACEMENT_3D ( 'NONE', #136719, #1879, #70099 ) ;
#107493=EDGE_LOOP ( 'NONE', ( #4000, #1577, #96601, #53771 ) ) ;
#107495=DIRECTION ( 'NONE',  ( -0.7071067811865486830, 0.7071067811865464625, 0.000000000000000000 ) ) ;
#107496=DIRECTION ( 'NONE',  ( 0.7071067811865486830, -0.7071067811865464625, -0.000000000000000000 ) ) ;
#107497=ADVANCED_FACE ( 'NONE', ( #67183 ), #466, .F. ) ;
#107498=AXIS2_PLACEMENT_3D ( 'NONE', #90359, #23680, #103357 ) ;
#107501=VECTOR ( 'NONE', #65442, 1000.000000000000000 ) ;
#107502=AXIS2_PLACEMENT_3D ( 'NONE', #73111, #117271, #29560 ) ;
#107503=DIRECTION ( 'NONE',  ( 0.7071067811865487940, 0.7071067811865463515, 0.000000000000000000 ) ) ;
#107504=LINE ( 'NONE', #28541, #134806 ) ;
#107507=CARTESIAN_POINT ( 'NONE',  ( 27.48921356237309155, -27.52281430457074762, 5.000000000000000000 ) ) ;
#107508=DIRECTION ( 'NONE',  ( 0.7071067811865487940, 0.7071067811865463515, -0.000000000000000000 ) ) ;
#107509=LINE ( 'NONE', #27094, #71431 ) ;
#107511=CARTESIAN_POINT ( 'NONE',  ( 31.99806943317879515, -22.22500000000000142, 4.500000000000000888 ) ) ;
#107513=ORIENTED_EDGE ( 'NONE', *, *, #42617, .F. ) ;
#107515=ORIENTED_EDGE ( 'NONE', *, *, #91318, .F. ) ;
#107516=EDGE_CURVE ( 'NONE', #126734, #92516, #109245, .T. ) ;
#107517=ORIENTED_EDGE ( 'NONE', *, *, #59895, .T. ) ;
#107518=CARTESIAN_POINT ( 'NONE',  ( 22.49999999999985079, 13.08746187583910725, 4.000000000000000000 ) ) ;
#107520=ORIENTED_EDGE ( 'NONE', *, *, #77848, .T. ) ;
#107521=EDGE_CURVE ( 'NONE', #113241, #12982, #121540, .T. ) ;
#107523=DIRECTION ( 'NONE',  ( 0.3543493200069162685, -0.000000000000000000, -0.9351131265310288487 ) ) ;
#107524=DIRECTION ( 'NONE',  ( -0.6830127018922181881, 0.6830127018922202975, -0.2588190451025214056 ) ) ;
#107525=DIRECTION ( 'NONE',  ( -0.6830127018922180770, -0.6830127018922204085, -0.2588190451025213501 ) ) ;
#107526=LINE ( 'NONE', #51745, #57017 ) ;
#107527=ORIENTED_EDGE ( 'NONE', *, *, #124349, .T. ) ;
#107528=DIRECTION ( 'NONE',  ( -0.000000000000000000, 0.3543493200069153248, 0.9351131265310292928 ) ) ;
#107530=CARTESIAN_POINT ( 'NONE',  ( -36.48921356237310221, -27.52281430457080802, 5.000000000000000000 ) ) ;
#107531=CARTESIAN_POINT ( 'NONE',  ( 0.000000000000000000, 0.000000000000000000, 5.000000000000000000 ) ) ;
#107532=FACE_OUTER_BOUND ( 'NONE', #106674, .T. ) ;
#107533=EDGE_CURVE ( 'NONE', #83048, #47602, #34555, .T. ) ;
#107536=DIRECTION ( 'NONE',  ( -0.7071067811865487940, 0.7071067811865463515, 0.000000000000000000 ) ) ;
#107537=ORIENTED_EDGE ( 'NONE', *, *, #114850, .F. ) ;
#107538=ORIENTED_EDGE ( 'NONE', *, *, #80977, .T. ) ;
#107540=CARTESIAN_POINT ( 'NONE',  ( 34.92499999999998295, 15.66246187583885963, 4.000000000000000000 ) ) ;
#107541=EDGE_CURVE ( 'NONE', #47692, #4072, #12065, .T. ) ;
#107542=CARTESIAN_POINT ( 'NONE',  ( -11.99999999999991118, -15.41253812416059787, 4.000000000000000000 ) ) ;
#107544=VERTEX_POINT ( 'NONE', #78780 ) ;
#107546=LINE ( 'NONE', #19818, #109422 ) ;
#107548=EDGE_LOOP ( 'NONE', ( #16192, #42642, #43992, #116261 ) ) ;
#107549=DIRECTION ( 'NONE',  ( -0.7071067811865486830, -0.7071067811865464625, 0.000000000000000000 ) ) ;
#107550=EDGE_LOOP ( 'NONE', ( #25709, #120637, #121848, #27390 ) ) ;
#107551=ORIENTED_EDGE ( 'NONE', *, *, #50056, .F. ) ;
#107552=PLANE ( 'NONE',  #90966 ) ;
#107554=LINE ( 'NONE', #96645, #9553 ) ;
#107556=ORIENTED_EDGE ( 'NONE', *, *, #3092, .T. ) ;
#107557=EDGE_CURVE ( 'NONE', #7557, #30943, #45457, .T. ) ;
#107559=DIRECTION ( 'NONE',  ( 1.000000000000000000, 0.000000000000000000, 0.000000000000000000 ) ) ;
#107560=VERTEX_POINT ( 'NONE', #131727 ) ;
#107561=ADVANCED_FACE ( 'NONE', ( #55602 ), #11321, .F. ) ;
#107563=CARTESIAN_POINT ( 'NONE',  ( 36.48921356237310221, -27.52281430457080802, 5.000000000000000000 ) ) ;
#107564=VECTOR ( 'NONE', #122787, 1000.000000000000000 ) ;
#107565=PLANE ( 'NONE',  #90081 ) ;
#107566=EDGE_LOOP ( 'NONE', ( #112126, #22795, #103786, #117647 ) ) ;
#107568=VERTEX_POINT ( 'NONE', #32417 ) ;
#107569=DIRECTION ( 'NONE',  ( 0.7071067811865487940, 0.7071067811865463515, -0.000000000000000000 ) ) ;
#107571=DIRECTION ( 'NONE',  ( 0.7071067811865487940, 0.7071067811865463515, 0.000000000000000000 ) ) ;
#107572=CARTESIAN_POINT ( 'NONE',  ( -21.48921356237309155, -27.52281430457070499, 5.000000000000000000 ) ) ;
#107574=ORIENTED_EDGE ( 'NONE', *, *, #95965, .F. ) ;
#107575=ORIENTED_EDGE ( 'NONE', *, *, #75762, .F. ) ;
#107576=DIRECTION ( 'NONE',  ( 0.7071067811865487940, -0.7071067811865463515, 0.000000000000000000 ) ) ;
#107578=ORIENTED_EDGE ( 'NONE', *, *, #16310, .F. ) ;
#107579=( BOUNDED_CURVE ( )  B_SPLINE_CURVE ( 3, ( #87701, #32629, #99258, #77568 ),
 .UNSPECIFIED., .F., .F. ) 
 B_SPLINE_CURVE_WITH_KNOTS ( ( 4, 4 ),
 ( 5.005968288816728951, 5.074607125596368284 ),
 .UNSPECIFIED. ) 
 CURVE ( )  GEOMETRIC_REPRESENTATION_ITEM ( )  RATIONAL_B_SPLINE_CURVE ( ( 1.000000000000000000, 0.9996074310407762065, 0.9996074310407762065, 1.000000000000000000 ) ) 
 REPRESENTATION_ITEM ( '' )  );
#107581=ORIENTED_EDGE ( 'NONE', *, *, #50531, .T. ) ;
#107583=VECTOR ( 'NONE', #125149, 1000.000000000000000 ) ;
#107585=ORIENTED_EDGE ( 'NONE', *, *, #102615, .T. ) ;
#107586=DIRECTION ( 'NONE',  ( 0.3543493200069162685, -0.000000000000000000, -0.9351131265310288487 ) ) ;
#107588=( BOUNDED_CURVE ( )  B_SPLINE_CURVE ( 3, ( #23461, #68441, #112620, #2393 ),
 .UNSPECIFIED., .F., .T. ) 
 B_SPLINE_CURVE_WITH_KNOTS ( ( 4, 4 ),
 ( 1.208578181583223055, 1.359146454359418055 ),
 .UNSPECIFIED. ) 
 CURVE ( )  GEOMETRIC_REPRESENTATION_ITEM ( )  RATIONAL_B_SPLINE_CURVE ( ( 1.000000000000000000, 0.9981116584018954185, 0.9981116584018954185, 1.000000000000000000 ) ) 
 REPRESENTATION_ITEM ( '' )  );
#107589=LINE ( 'NONE', #130809, #30399 ) ;
#107590=FACE_BOUND ( 'NONE', #111823, .T. ) ;
#107591=EDGE_CURVE ( 'NONE', #85633, #90206, #138698, .T. ) ;
#107592=DIRECTION ( 'NONE',  ( -0.3543493200069162685, -0.000000000000000000, -0.9351131265310288487 ) ) ;
#107593=PLANE ( 'NONE',  #49010 ) ;
#107594=CARTESIAN_POINT ( 'NONE',  ( 23.99999999999983302, -19.22509904557634286, 1.855685503482233933 ) ) ;
#107595=DIRECTION ( 'NONE',  ( 0.6830127018922181881, 0.6830127018922202975, -0.2588190451025214056 ) ) ;
#107596=VERTEX_POINT ( 'NONE', #139429 ) ;
#107599=ORIENTED_EDGE ( 'NONE', *, *, #93346, .F. ) ;
#107600=VECTOR ( 'NONE', #123846, 1000.000000000000000 ) ;
#107602=ORIENTED_EDGE ( 'NONE', *, *, #134166, .T. ) ;
#107604=ORIENTED_EDGE ( 'NONE', *, *, #75166, .T. ) ;
#107605=FACE_OUTER_BOUND ( 'NONE', #98381, .T. ) ;
#107607=DIRECTION ( 'NONE',  ( 0.7071067811865487940, 0.7071067811865463515, 0.000000000000000000 ) ) ;
#107608=DIRECTION ( 'NONE',  ( -0.7071067811865486830, -0.7071067811865464625, 0.000000000000000000 ) ) ;
#107609=DIRECTION ( 'NONE',  ( -0.000000000000000000, -0.3543493200069152138, 0.9351131265310292928 ) ) ;
#107610=LINE ( 'NONE', #53987, #34522 ) ;
#107611=PLANE ( 'NONE',  #128781 ) ;
#107612=CARTESIAN_POINT ( 'NONE',  ( -14.99999999999990230, 7.007997736742436423, -8.085015511992146742 ) ) ;
#107613=DIRECTION ( 'NONE',  ( -0.7071067811865486830, -0.7071067811865464625, 0.000000000000000000 ) ) ;
#107614=CARTESIAN_POINT ( 'NONE',  ( -24.18398860626899705, 28.73617430169804265, 5.000000000000000000 ) ) ;
#107615=DIRECTION ( 'NONE',  ( -0.7071067811865486830, -0.7071067811865464625, 0.000000000000000000 ) ) ;
#107617=DIRECTION ( 'NONE',  ( -0.7071067811865487940, 0.7071067811865463515, -0.000000000000000000 ) ) ;
#107618=ORIENTED_EDGE ( 'NONE', *, *, #129201, .F. ) ;
#107619=LINE ( 'NONE', #8279, #42614 ) ;
#107620=CARTESIAN_POINT ( 'NONE',  ( 1.734723475976807094E-15, -0.03360074219774071558, 5.000000000000000000 ) ) ;
#107621=ORIENTED_EDGE ( 'NONE', *, *, #43631, .F. ) ;
#107622=ORIENTED_EDGE ( 'NONE', *, *, #60211, .F. ) ;
#107623=ORIENTED_EDGE ( 'NONE', *, *, #4994, .T. ) ;
#107627=EDGE_CURVE ( 'NONE', #89442, #76045, #94445, .T. ) ;
#107631=ORIENTED_EDGE ( 'NONE', *, *, #12363, .F. ) ;
#107633=CARTESIAN_POINT ( 'NONE',  ( 0.000000000000000000, 0.000000000000000000, 5.000000000000000000 ) ) ;
#107634=EDGE_CURVE ( 'NONE', #126278, #63804, #25804, .T. ) ;
#107635=ORIENTED_EDGE ( 'NONE', *, *, #2838, .F. ) ;
#107636=LINE ( 'NONE', #30827, #69637 ) ;
#107637=DIRECTION ( 'NONE',  ( 0.6830127018922180770, -0.6830127018922204085, -0.2588190451025213501 ) ) ;
#107638=CARTESIAN_POINT ( 'NONE',  ( -45.18398860626900415, 28.73617430169818832, 5.000000000000000000 ) ) ;
#107639=VERTEX_POINT ( 'NONE', #14212 ) ;
#107641=EDGE_CURVE ( 'NONE', #119366, #64166, #57756, .T. ) ;
#107642=CARTESIAN_POINT ( 'NONE',  ( 10.49999999999992539, -11.56887692260769640, 4.000000000000000000 ) ) ;
#107643=CARTESIAN_POINT ( 'NONE',  ( -9.183988606268997046, 28.73617430169793607, 5.000000000000000000 ) ) ;
#107644=EDGE_LOOP ( 'NONE', ( #133312, #133662, #47800, #140767 ) ) ;
#107645=FACE_OUTER_BOUND ( 'NONE', #42362, .T. ) ;
#107646=ORIENTED_EDGE ( 'NONE', *, *, #113153, .F. ) ;
#107647=ORIENTED_EDGE ( 'NONE', *, *, #74422, .F. ) ;
#107648=VERTEX_POINT ( 'NONE', #106015 ) ;
#107649=ADVANCED_FACE ( 'NONE', ( #84330 ), #47610, .F. ) ;
#107651=DIRECTION ( 'NONE',  ( 0.6830127018922181881, 0.6830127018922202975, -0.2588190451025214056 ) ) ;
#107652=DIRECTION ( 'NONE',  ( -0.7071067811865487940, 0.7071067811865463515, -0.000000000000000000 ) ) ;
#107653=EDGE_CURVE ( 'NONE', #130333, #91901, #40115, .T. ) ;
#107654=LINE ( 'NONE', #8314, #37887 ) ;
#107655=FACE_OUTER_BOUND ( 'NONE', #60872, .T. ) ;
#107656=EDGE_CURVE ( 'NONE', #38538, #74972, #123725, .T. ) ;
#107658=ORIENTED_EDGE ( 'NONE', *, *, #49747, .T. ) ;
#107659=CARTESIAN_POINT ( 'NONE',  ( 32.67183060077623225, -18.74070752338409562, 4.000000000000000000 ) ) ;
#107660=ORIENTED_EDGE ( 'NONE', *, *, #105049, .F. ) ;
#107661=DIRECTION ( 'NONE',  ( -0.3543493200069163240, 0.000000000000000000, 0.9351131265310288487 ) ) ;
#107663=VECTOR ( 'NONE', #42683, 1000.000000000000000 ) ;
#107665=ORIENTED_EDGE ( 'NONE', *, *, #42233, .F. ) ;
#107666=DIRECTION ( 'NONE',  ( -0.3543493200069162685, -0.000000000000000000, -0.9351131265310288487 ) ) ;
#107667=DIRECTION ( 'NONE',  ( 1.000000000000000000, 0.000000000000000000, 0.000000000000000000 ) ) ;
#107668=ORIENTED_EDGE ( 'NONE', *, *, #4673, .F. ) ;
#107669=VECTOR ( 'NONE', #125950, 1000.000000000000000 ) ;
#107670=EDGE_LOOP ( 'NONE', ( #50592, #90153, #13088, #60910 ) ) ;
#107672=LINE ( 'NONE', #95372, #23314 ) ;
#107673=DIRECTION ( 'NONE',  ( 0.7071067811865486830, -0.7071067811865464625, -0.000000000000000000 ) ) ;
#107674=LINE ( 'NONE', #75092, #14953 ) ;
#107675=CARTESIAN_POINT ( 'NONE',  ( 22.00193056682082826, -22.22500000000000142, 4.500000000000000888 ) ) ;
#107677=CARTESIAN_POINT ( 'NONE',  ( 39.18398860626899705, 28.73617430169814568, 5.000000000000000000 ) ) ;
#107678=VECTOR ( 'NONE', #31218, 999.9999999999998863 ) ;
#107680=DIRECTION ( 'NONE',  ( 0.7071067811865486830, -0.7071067811865464625, -0.000000000000000000 ) ) ;
#107681=ORIENTED_EDGE ( 'NONE', *, *, #105314, .T. ) ;
#107682=DIRECTION ( 'NONE',  ( 1.000000000000000000, 0.000000000000000000, 0.000000000000000000 ) ) ;
#107684=VERTEX_POINT ( 'NONE', #40704 ) ;
#107685=FACE_OUTER_BOUND ( 'NONE', #57363, .T. ) ;
#107687=ORIENTED_EDGE ( 'NONE', *, *, #96638, .T. ) ;
#107688=DIRECTION ( 'NONE',  ( -0.6830127018922180770, -0.6830127018922204085, -0.2588190451025214056 ) ) ;
#107689=FACE_OUTER_BOUND ( 'NONE', #40739, .T. ) ;
#107691=CARTESIAN_POINT ( 'NONE',  ( 42.18398860626899705, 28.73617430169816700, 5.000000000000000000 ) ) ;
#107692=PLANE ( 'NONE',  #37073 ) ;
#107693=LINE ( 'NONE', #62802, #8308 ) ;
#107694=ORIENTED_EDGE ( 'NONE', *, *, #24593, .T. ) ;
#107695=ADVANCED_FACE ( 'NONE', ( #118956 ), #84906, .T. ) ;
#107696=ORIENTED_EDGE ( 'NONE', *, *, #77766, .T. ) ;
#107698=DIRECTION ( 'NONE',  ( -0.6830127018922180770, -0.6830127018922204085, -0.2588190451025213501 ) ) ;
#107699=DIRECTION ( 'NONE',  ( 0.7071067811865486830, -0.7071067811865464625, -0.000000000000000000 ) ) ;
#107703=VECTOR ( 'NONE', #19908, 1000.000000000000114 ) ;
#107704=LINE ( 'NONE', #8362, #20561 ) ;
#107706=AXIS2_PLACEMENT_3D ( 'NONE', #76380, #65534, #130043 ) ;
#107707=LINE ( 'NONE', #8364, #95502 ) ;
#107708=EDGE_CURVE ( 'NONE', #46912, #71167, #42145, .T. ) ;
#107709=CARTESIAN_POINT ( 'NONE',  ( 30.48921356237309510, -27.52281430457076894, 5.000000000000000000 ) ) ;
#107711=ORIENTED_EDGE ( 'NONE', *, *, #115973, .F. ) ;
#107712=CARTESIAN_POINT ( 'NONE',  ( 0.000000000000000000, 0.000000000000000000, 5.000000000000000000 ) ) ;
#107713=ORIENTED_EDGE ( 'NONE', *, *, #33416, .T. ) ;
#107716=CARTESIAN_POINT ( 'NONE',  ( -14.29289321881335795, 8.259292476615634371, 5.000000000000000000 ) ) ;
#107717=CARTESIAN_POINT ( 'NONE',  ( 8.999999999999937828, -0.2811185226894198363, -5.995736974527534180 ) ) ;
#107718=EDGE_LOOP ( 'NONE', ( #120283, #95322, #84716 ) ) ;
#107719=CARTESIAN_POINT ( 'NONE',  ( 27.48921356237309155, -27.52281430457074762, 5.000000000000000000 ) ) ;
#107720=DIRECTION ( 'NONE',  ( -0.7071067811865487940, 0.7071067811865463515, 0.000000000000000000 ) ) ;
#107721=LINE ( 'NONE', #130221, #46390 ) ;
#107722=EDGE_CURVE ( 'NONE', #67449, #111297, #19646, .T. ) ;
#107723=DIRECTION ( 'NONE',  ( 1.000000000000000000, 0.000000000000000000, 0.000000000000000000 ) ) ;
#107724=DIRECTION ( 'NONE',  ( 0.7071067811865486830, -0.7071067811865464625, -0.000000000000000000 ) ) ;
#107727=DIRECTION ( 'NONE',  ( -0.3543493200069162685, -0.000000000000000000, -0.9351131265310288487 ) ) ;
#107728=DIRECTION ( 'NONE',  ( 1.000000000000000000, 0.000000000000000000, 0.000000000000000000 ) ) ;
#107730=ORIENTED_EDGE ( 'NONE', *, *, #39651, .T. ) ;
#107731=ORIENTED_EDGE ( 'NONE', *, *, #56125, .T. ) ;
#107734=CARTESIAN_POINT ( 'NONE',  ( 18.53421140649331633, 9.121673282332597665, 4.000000000000000000 ) ) ;
#107736=CARTESIAN_POINT ( 'NONE',  ( 8.673617379884035472E-16, 16.55218569542899587, 5.000000000000000000 ) ) ;
#107738=ORIENTED_EDGE ( 'NONE', *, *, #111158, .T. ) ;
#107739=LINE ( 'NONE', #71574, #37581 ) ;
#107740=CARTESIAN_POINT ( 'NONE',  ( 21.29974487139158512, -27.71228299555221142, 4.000000000000000000 ) ) ;
#107742=EDGE_CURVE ( 'NONE', #76469, #63599, #99328, .T. ) ;
#107744=DIRECTION ( 'NONE',  ( -0.7071067811865486830, 0.7071067811865464625, 0.000000000000000000 ) ) ;
#107746=FACE_OUTER_BOUND ( 'NONE', #75271, .T. ) ;
#107747=EDGE_LOOP ( 'NONE', ( #143482, #95897, #112962, #28182 ) ) ;
#107748=EDGE_LOOP ( 'NONE', ( #101610, #29615, #5757, #86727 ) ) ;
#107749=EDGE_CURVE ( 'NONE', #123709, #111380, #67475, .T. ) ;
#107750=FACE_BOUND ( 'NONE', #102601, .T. ) ;
#107751=EDGE_CURVE ( 'NONE', #2559, #66501, #13035, .T. ) ;
#107752=FACE_OUTER_BOUND ( 'NONE', #55410, .T. ) ;
#107753=CYLINDRICAL_SURFACE ( 'NONE', #21148, 0.5000000000000004441 ) ;
#107754=CARTESIAN_POINT ( 'NONE',  ( -21.62762920772360786, 8.558752285115851066, 4.000000000000000000 ) ) ;
#107758=VECTOR ( 'NONE', #123645, 1000.000000000000000 ) ;
#107759=ORIENTED_EDGE ( 'NONE', *, *, #126904, .T. ) ;
#107760=EDGE_LOOP ( 'NONE', ( #85643, #29390, #142723, #56700 ) ) ;
#107761=ORIENTED_EDGE ( 'NONE', *, *, #48089, .T. ) ;
#107763=VERTEX_POINT ( 'NONE', #101487 ) ;
#107764=EDGE_CURVE ( 'NONE', #43048, #46174, #123277, .T. ) ;
#107765=LINE ( 'NONE', #52682, #110350 ) ;
#107766=DIRECTION ( 'NONE',  ( 1.000000000000000000, 0.000000000000000000, 0.000000000000000000 ) ) ;
#107767=ORIENTED_EDGE ( 'NONE', *, *, #34508, .T. ) ;
#107768=VECTOR ( 'NONE', #10672, 1000.000000000000000 ) ;
#107770=CARTESIAN_POINT ( 'NONE',  ( 32.29387692260782217, 22.22500000000000142, 4.000000000000000000 ) ) ;
#107771=CARTESIAN_POINT ( 'NONE',  ( -48.18398860626899705, 28.73617430169820608, 5.000000000000000000 ) ) ;
#107772=LINE ( 'NONE', #72361, #6736 ) ;
#107774=ORIENTED_EDGE ( 'NONE', *, *, #108077, .T. ) ;
#107775=LINE ( 'NONE', #41831, #26451 ) ;
#107776=CARTESIAN_POINT ( 'NONE',  ( -2.510786437626908008, -27.52281430457053446, 5.000000000000000000 ) ) ;
#107777=ORIENTED_EDGE ( 'NONE', *, *, #44690, .T. ) ;
#107778=DIRECTION ( 'NONE',  ( -0.6830127018922180770, -0.6830127018922204085, -0.2588190451025213501 ) ) ;
#107779=ORIENTED_EDGE ( 'NONE', *, *, #117251, .T. ) ;
#107780=ORIENTED_EDGE ( 'NONE', *, *, #73165, .F. ) ;
#107781=ORIENTED_EDGE ( 'NONE', *, *, #112277, .F. ) ;
#107783=VERTEX_POINT ( 'NONE', #80481 ) ;
#107784=ORIENTED_EDGE ( 'NONE', *, *, #4962, .F. ) ;
#107785=VECTOR ( 'NONE', #64977, 1000.000000000000227 ) ;
#107786=DIRECTION ( 'NONE',  ( 0.7071067811865487940, -0.7071067811865463515, 0.000000000000000000 ) ) ;
#107787=VECTOR ( 'NONE', #21448, 1000.000000000000000 ) ;
#107788=EDGE_CURVE ( 'NONE', #55935, #124530, #124675, .T. ) ;
#107789=PLANE ( 'NONE',  #130714 ) ;
#107791=CARTESIAN_POINT ( 'NONE',  ( -18.77004279457780811, 21.73644205237998506, 5.000000000000000888 ) ) ;
#107792=AXIS2_PLACEMENT_3D ( 'NONE', #16721, #83426, #60999 ) ;
#107793=ADVANCED_FACE ( 'NONE', ( #89895 ), #113072, .F. ) ;
#107794=CARTESIAN_POINT ( 'NONE',  ( -60.18398860626900415, 28.73617430169829490, 5.000000000000000000 ) ) ;
#107795=CARTESIAN_POINT ( 'NONE',  ( -0.3281693992235250046, -21.74070752338406365, 4.000000000000000000 ) ) ;
#107796=AXIS2_PLACEMENT_3D ( 'NONE', #17122, #61390, #83844 ) ;
#107798=ADVANCED_FACE ( 'NONE', ( #102233 ), #112381, .F. ) ;
#107800=DIRECTION ( 'NONE',  ( 0.7071067811865487940, 0.7071067811865463515, -0.000000000000000000 ) ) ;
#107801=CARTESIAN_POINT ( 'NONE',  ( -34.42500000000001137, 2.977185695429387824, 5.000000000000000000 ) ) ;
#107802=ORIENTED_EDGE ( 'NONE', *, *, #57619, .F. ) ;
#107803=FACE_OUTER_BOUND ( 'NONE', #33262, .T. ) ;
#107805=VERTEX_POINT ( 'NONE', #33427 ) ;
#107806=EDGE_LOOP ( 'NONE', ( #32898, #12418, #79897, #18872 ) ) ;
#107807=EDGE_LOOP ( 'NONE', ( #125254, #66975, #1512, #83150 ) ) ;
#107809=PLANE ( 'NONE',  #98830 ) ;
#107814=ORIENTED_EDGE ( 'NONE', *, *, #58973, .T. ) ;
#107818=DIRECTION ( 'NONE',  ( -0.3543493200069162685, -0.000000000000000000, -0.9351131265310288487 ) ) ;
#107821=ORIENTED_EDGE ( 'NONE', *, *, #122611, .T. ) ;
#107823=LINE ( 'NONE', #83994, #111216 ) ;
#107824=CARTESIAN_POINT ( 'NONE',  ( -2.816011393730999401, 28.73617430169785436, 5.000000000000000000 ) ) ;
#107825=EDGE_CURVE ( 'NONE', #129495, #22625, #12334, .T. ) ;
#107826=PLANE ( 'NONE',  #114415 ) ;
#107827=FACE_OUTER_BOUND ( 'NONE', #21558, .T. ) ;
#107828=LINE ( 'NONE', #20828, #78165 ) ;
#107831=CARTESIAN_POINT ( 'NONE',  ( -45.48921356237309510, -27.52281430457087197, 5.000000000000000000 ) ) ;
#107832=CARTESIAN_POINT ( 'NONE',  ( -18.18398860626898994, 28.73617430169800002, 5.000000000000000000 ) ) ;
#107833=ORIENTED_EDGE ( 'NONE', *, *, #41024, .T. ) ;
#107834=CARTESIAN_POINT ( 'NONE',  ( 34.92499999999998295, -6.183345613589489531, 4.500000000000000888 ) ) ;
#107836=DIRECTION ( 'NONE',  ( 0.3543493200069162685, -0.000000000000000000, -0.9351131265310288487 ) ) ;
#107837=EDGE_LOOP ( 'NONE', ( #74079, #24521, #101634, #33785 ) ) ;
#107838=CARTESIAN_POINT ( 'NONE',  ( -21.70710678118638270, -18.74070752338409562, 5.000000000000000000 ) ) ;
#107840=VERTEX_POINT ( 'NONE', #47867 ) ;
#107842=EDGE_CURVE ( 'NONE', #95326, #87449, #48546, .T. ) ;
#107843=ORIENTED_EDGE ( 'NONE', *, *, #31680, .F. ) ;
#107844=CARTESIAN_POINT ( 'NONE',  ( 14.99999999999989519, -16.06887692260765377, 4.000000000000000000 ) ) ;
#107845=ADVANCED_FACE ( 'NONE', ( #136982 ), #58765, .F. ) ;
#107846=VERTEX_POINT ( 'NONE', #4249 ) ;
#107847=VERTEX_POINT ( 'NONE', #94874 ) ;
#107848=EDGE_CURVE ( 'NONE', #58070, #108960, #139135, .T. ) ;
#107851=LINE ( 'NONE', #120143, #104037 ) ;
#107852=CARTESIAN_POINT ( 'NONE',  ( -24.29974487139158867, -27.71228299555223273, 4.000000000000000000 ) ) ;
#107854=DIRECTION ( 'NONE',  ( -0.3543493200069162685, -0.000000000000000000, -0.9351131265310288487 ) ) ;
#107855=DIRECTION ( 'NONE',  ( 0.7071067811865486830, -0.7071067811865464625, -0.000000000000000000 ) ) ;
#107856=DIRECTION ( 'NONE',  ( 0.6830127018922181881, 0.6830127018922202975, -0.2588190451025214056 ) ) ;
#107859=DIRECTION ( 'NONE',  ( 0.7071067811865487940, -0.7071067811865463515, 0.000000000000000000 ) ) ;
#107860=DIRECTION ( 'NONE',  ( -0.000000000000000000, -0.000000000000000000, 1.000000000000000000 ) ) ;
#107861=ORIENTED_EDGE ( 'NONE', *, *, #20911, .F. ) ;
#107862=ORIENTED_EDGE ( 'NONE', *, *, #32376, .F. ) ;
#107863=DIRECTION ( 'NONE',  ( -0.000000000000000000, 0.3543493200069153248, 0.9351131265310292928 ) ) ;
#107864=VERTEX_POINT ( 'NONE', #71033 ) ;
#107865=VECTOR ( 'NONE', #106798, 1000.000000000000000 ) ;
#107866=PLANE ( 'NONE',  #138289 ) ;
#107867=LINE ( 'NONE', #64395, #138971 ) ;
#107869=ORIENTED_EDGE ( 'NONE', *, *, #34369, .F. ) ;
#107870=LINE ( 'NONE', #98452, #81266 ) ;
#107871=CARTESIAN_POINT ( 'NONE',  ( 29.99451991528749417, 28.92564299267958816, 4.000000000000000000 ) ) ;
#107874=PLANE ( 'NONE',  #21983 ) ;
#107875=VERTEX_POINT ( 'NONE', #71743 ) ;
#107880=AXIS2_PLACEMENT_3D ( 'NONE', #110402, #35040, #45910 ) ;
#107882=EDGE_LOOP ( 'NONE', ( #69140, #109396, #36923, #59125 ) ) ;
#107883=ORIENTED_EDGE ( 'NONE', *, *, #28598, .F. ) ;
#107884=ORIENTED_EDGE ( 'NONE', *, *, #5937, .F. ) ;
#107885=VECTOR ( 'NONE', #46651, 999.9999999999998863 ) ;
#107887=ORIENTED_EDGE ( 'NONE', *, *, #29306, .T. ) ;
#107888=AXIS2_PLACEMENT_3D ( 'NONE', #39094, #105056, #16610 ) ;
#107890=AXIS2_PLACEMENT_3D ( 'NONE', #107341, #67442, #76897 ) ;
#107892=ORIENTED_EDGE ( 'NONE', *, *, #87166, .F. ) ;
#107896=ORIENTED_EDGE ( 'NONE', *, *, #54310, .T. ) ;
#107898=CARTESIAN_POINT ( 'NONE',  ( 5.999999999999955591, -21.84840872380824095, 2.849755605029621996 ) ) ;
#107899=CARTESIAN_POINT ( 'NONE',  ( 19.05000000000000071, 3.174999999999997158, 5.000000000000000000 ) ) ;
#107900=PLANE ( 'NONE',  #9113 ) ;
#107901=ORIENTED_EDGE ( 'NONE', *, *, #4508, .F. ) ;
#107902=VERTEX_POINT ( 'NONE', #49289 ) ;
#107904=VERTEX_POINT ( 'NONE', #37688 ) ;
#107905=CARTESIAN_POINT ( 'NONE',  ( 27.60486233187505078, 21.75929247661550647, 21.32995629748180377 ) ) ;
#107906=ADVANCED_FACE ( 'NONE', ( #115903 ), #84059, .F. ) ;
#107907=PLANE ( 'NONE',  #98664 ) ;
#107910=DIRECTION ( 'NONE',  ( -0.7071067811865486830, -0.7071067811865464625, 0.000000000000000000 ) ) ;
#107912=ORIENTED_EDGE ( 'NONE', *, *, #137910, .T. ) ;
#107914=VERTEX_POINT ( 'NONE', #125401 ) ;
#107915=PLANE ( 'NONE',  #1598 ) ;
#107916=ORIENTED_EDGE ( 'NONE', *, *, #5579, .T. ) ;
#107917=ORIENTED_EDGE ( 'NONE', *, *, #56944, .F. ) ;
#107918=VECTOR ( 'NONE', #48354, 1000.000000000000227 ) ;
#107919=EDGE_CURVE ( 'NONE', #81042, #137586, #81928, .T. ) ;
#107920=DIRECTION ( 'NONE',  ( -0.000000000000000000, 0.000000000000000000, 1.000000000000000000 ) ) ;
#107921=CARTESIAN_POINT ( 'NONE',  ( 59.99451991528749772, 28.92564299267980132, 4.000000000000000000 ) ) ;
#107922=ORIENTED_EDGE ( 'NONE', *, *, #12758, .T. ) ;
#107924=CARTESIAN_POINT ( 'NONE',  ( -17.52663903635773934, -5.240707523384225297, 16.25846745537491600 ) ) ;
#107925=VECTOR ( 'NONE', #3882, 999.9999999999998863 ) ;
#107926=CARTESIAN_POINT ( 'NONE',  ( 24.91272823266826109, 2.053671025133813277, 5.000000000000000000 ) ) ;
#107927=EDGE_CURVE ( 'NONE', #139716, #138830, #83321, .T. ) ;
#107928=PLANE ( 'NONE',  #81448 ) ;
#107929=EDGE_LOOP ( 'NONE', ( #101379, #119452, #59250, #16799 ) ) ;
#107931=EDGE_LOOP ( 'NONE', ( #75895, #26409, #91499, #23664 ) ) ;
#107933=DIRECTION ( 'NONE',  ( 0.7071067811865487940, -0.7071067811865463515, 0.000000000000000000 ) ) ;
#107934=ORIENTED_EDGE ( 'NONE', *, *, #3947, .T. ) ;
#107935=CARTESIAN_POINT ( 'NONE',  ( -45.18398860626900415, 28.73617430169818832, 5.000000000000000000 ) ) ;
#107936=EDGE_LOOP ( 'NONE', ( #16871, #88646, #80041, #37609 ) ) ;
#107937=CARTESIAN_POINT ( 'NONE',  ( 29.99999999999979039, -13.97847968911257865, -0.1324546996126097498 ) ) ;
#107940=ORIENTED_EDGE ( 'NONE', *, *, #13577, .F. ) ;
#107941=VECTOR ( 'NONE', #47580, 1000.000000000000000 ) ;
#107948=DIRECTION ( 'NONE',  ( 0.7071067811865487940, 0.7071067811865463515, 0.000000000000000000 ) ) ;
#107949=CARTESIAN_POINT ( 'NONE',  ( 42.48921356237308800, -27.52281430457085065, 5.000000000000000000 ) ) ;
#107950=EDGE_CURVE ( 'NONE', #30447, #23039, #92033, .T. ) ;
#107951=ADVANCED_FACE ( 'NONE', ( #81191 ), #26087, .T. ) ;
#107952=DIRECTION ( 'NONE',  ( -0.000000000000000000, 0.3543493200069153248, 0.9351131265310292928 ) ) ;
#107953=CARTESIAN_POINT ( 'NONE',  ( 44.99451991528749772, 28.92564299267969474, 4.000000000000000000 ) ) ;
#107954=DIRECTION ( 'NONE',  ( 0.6830127018922180770, -0.6830127018922204085, -0.2588190451025213501 ) ) ;
#107956=ORIENTED_EDGE ( 'NONE', *, *, #105538, .T. ) ;
#107957=ORIENTED_EDGE ( 'NONE', *, *, #68612, .T. ) ;
#107958=ORIENTED_EDGE ( 'NONE', *, *, #113959, .T. ) ;
#107960=ORIENTED_EDGE ( 'NONE', *, *, #89308, .F. ) ;
#107961=EDGE_CURVE ( 'NONE', #28405, #139749, #6402, .T. ) ;
#107962=ORIENTED_EDGE ( 'NONE', *, *, #63822, .F. ) ;
#107963=FACE_OUTER_BOUND ( 'NONE', #43999, .T. ) ;
#107965=ADVANCED_FACE ( 'NONE', ( #26783 ), #59453, .F. ) ;
#107966=EDGE_CURVE ( 'NONE', #65370, #101800, #114494, .T. ) ;
#107967=LINE ( 'NONE', #130495, #32355 ) ;
#107969=DIRECTION ( 'NONE',  ( 0.6830127018922180770, -0.6830127018922204085, -0.2588190451025213501 ) ) ;
#107970=ORIENTED_EDGE ( 'NONE', *, *, #53483, .T. ) ;
#107971=VECTOR ( 'NONE', #127368, 999.9999999999998863 ) ;
#107972=VECTOR ( 'NONE', #205, 1000.000000000000000 ) ;
#107973=DIRECTION ( 'NONE',  ( -0.7071067811865486830, -0.7071067811865464625, -0.000000000000000000 ) ) ;
#107974=DIRECTION ( 'NONE',  ( 0.7071067811865487940, 0.7071067811865463515, -0.000000000000000000 ) ) ;
#107975=VECTOR ( 'NONE', #114278, 1000.000000000000000 ) ;
#107976=EDGE_CURVE ( 'NONE', #32821, #13806, #106719, .T. ) ;
#107978=ORIENTED_EDGE ( 'NONE', *, *, #71081, .F. ) ;
#107980=VECTOR ( 'NONE', #105531, 1000.000000000000000 ) ;
#107981=EDGE_CURVE ( 'NONE', #134825, #45274, #126794, .T. ) ;
#107982=CARTESIAN_POINT ( 'NONE',  ( 29.99999999999979039, -8.151047557385043163, -8.977947279169871564 ) ) ;
#107983=DIRECTION ( 'NONE',  ( -0.7071067811865486830, -0.7071067811865464625, 0.000000000000000000 ) ) ;
#107984=DIRECTION ( 'NONE',  ( -0.6830127018922181881, 0.6830127018922202975, -0.2588190451025214056 ) ) ;
#107985=ORIENTED_EDGE ( 'NONE', *, *, #64110, .T. ) ;
#107986=ORIENTED_EDGE ( 'NONE', *, *, #97188, .T. ) ;
#107987=LINE ( 'NONE', #76115, #63558 ) ;
#107988=ORIENTED_EDGE ( 'NONE', *, *, #93098, .F. ) ;
#107989=CARTESIAN_POINT ( 'NONE',  ( -13.49999999999990052, -13.91253812416061386, 4.000000000000000000 ) ) ;
#107990=CARTESIAN_POINT ( 'NONE',  ( -34.92500000000001137, -1.545334305399999275, 14.00746825007385610 ) ) ;
#107992=CARTESIAN_POINT ( 'NONE',  ( 30.18398860626900060, 28.73617430169808173, 5.000000000000000000 ) ) ;
#107993=EDGE_CURVE ( 'NONE', #13678, #35612, #40535, .T. ) ;
#107994=DIRECTION ( 'NONE',  ( -0.7071067811865486830, 0.7071067811865464625, 0.000000000000000000 ) ) ;
#107996=ORIENTED_EDGE ( 'NONE', *, *, #132909, .T. ) ;
#107997=DIRECTION ( 'NONE',  ( 0.7071067811865487940, 0.7071067811865463515, 0.000000000000000000 ) ) ;
#107999=CARTESIAN_POINT ( 'NONE',  ( -4.828169399223496860, 21.75929247661549581, 4.000000000000000000 ) ) ;
#108000=VERTEX_POINT ( 'NONE', #143219 ) ;
#108001=FACE_OUTER_BOUND ( 'NONE', #100806, .T. ) ;
#108002=CARTESIAN_POINT ( 'NONE',  ( -2.816011393730999401, 28.73617430169785436, 5.000000000000000000 ) ) ;
#108003=VERTEX_POINT ( 'NONE', #22827 ) ;
#108004=CARTESIAN_POINT ( 'NONE',  ( -75.48921356237309510, -27.52281430457107803, 5.000000000000000000 ) ) ;
#108006=ORIENTED_EDGE ( 'NONE', *, *, #130799, .T. ) ;
#108008=DIRECTION ( 'NONE',  ( -0.000000000000000000, 0.3543493200069152138, -0.9351131265310292928 ) ) ;
#108009=EDGE_CURVE ( 'NONE', #123934, #138063, #10538, .T. ) ;
#108010=ORIENTED_EDGE ( 'NONE', *, *, #93606, .F. ) ;
#108011=FACE_OUTER_BOUND ( 'NONE', #96347, .T. ) ;
#108012=ADVANCED_FACE ( 'NONE', ( #109874 ), #132383, .F. ) ;
#108013=DIRECTION ( 'NONE',  ( 1.000000000000000000, 0.000000000000000000, 0.000000000000000000 ) ) ;
#108014=EDGE_CURVE ( 'NONE', #39257, #141363, #55514, .T. ) ;
#108015=AXIS2_PLACEMENT_3D ( 'NONE', #20981, #108676, #42774 ) ;
#108016=CARTESIAN_POINT ( 'NONE',  ( 26.86500426248361606, 3.759292476615681888, 15.36553568819720006 ) ) ;
#108017=DIRECTION ( 'NONE',  ( -0.3543493200069162685, -0.000000000000000000, -0.9351131265310288487 ) ) ;
#108022=CARTESIAN_POINT ( 'NONE',  ( -20.99999999999984368, 14.96639925780210767, 5.000000000000000000 ) ) ;
#108024=VECTOR ( 'NONE', #128440, 1000.000000000000227 ) ;
#108025=DIRECTION ( 'NONE',  ( -0.7071067811865486830, -0.7071067811865464625, 0.000000000000000000 ) ) ;
#108026=ADVANCED_FACE ( 'NONE', ( #43211 ), #33077, .T. ) ;
#108027=DIRECTION ( 'NONE',  ( 0.7071067811865487940, 0.7071067811865463515, 0.000000000000000000 ) ) ;
#108028=ORIENTED_EDGE ( 'NONE', *, *, #83176, .T. ) ;
#108030=VERTEX_POINT ( 'NONE', #45373 ) ;
#108032=ORIENTED_EDGE ( 'NONE', *, *, #23391, .F. ) ;
#108033=EDGE_LOOP ( 'NONE', ( #101354, #9973, #86748, #53062 ) ) ;
#108034=EDGE_LOOP ( 'NONE', ( #72949, #48942, #50993, #71444 ) ) ;
#108035=VECTOR ( 'NONE', #63348, 1000.000000000000227 ) ;
#108037=CARTESIAN_POINT ( 'NONE',  ( 34.92190055902133849, 21.78725130426366974, 4.173570450635243567 ) ) ;
#108038=EDGE_LOOP ( 'NONE', ( #10986, #81810, #48031, #105489 ) ) ;
#108039=DIRECTION ( 'NONE',  ( 0.7071067811865487940, 0.7071067811865463515, -0.000000000000000000 ) ) ;
#108040=PLANE ( 'NONE',  #71856 ) ;
#108041=DIRECTION ( 'NONE',  ( -0.000000000000000000, 0.000000000000000000, 1.000000000000000000 ) ) ;
#108042=AXIS2_PLACEMENT_3D ( 'NONE', #66614, #64457, #8594 ) ;
#108043=DIRECTION ( 'NONE',  ( -0.7071067811865486830, -0.7071067811865464625, -0.000000000000000000 ) ) ;
#108045=ORIENTED_EDGE ( 'NONE', *, *, #30090, .T. ) ;
#108047=CARTESIAN_POINT ( 'NONE',  ( -34.92500000000001137, 22.22500000000000142, 4.000000000000000000 ) ) ;
#108048=CARTESIAN_POINT ( 'NONE',  ( 0.000000000000000000, 0.000000000000000000, 5.000000000000000000 ) ) ;
#108050=CARTESIAN_POINT ( 'NONE',  ( 32.67183060077624646, -6.740707523384209310, 4.000000000000000000 ) ) ;
#108051=CARTESIAN_POINT ( 'NONE',  ( -23.99451991528749062, 28.92564299267954908, 4.000000000000000000 ) ) ;
#108053=AXIS2_PLACEMENT_3D ( 'NONE', #8105, #142933, #130656 ) ;
#108055=VERTEX_POINT ( 'NONE', #128257 ) ;
#108056=EDGE_LOOP ( 'NONE', ( #262, #112828, #111401, #37266 ) ) ;
#108058=ORIENTED_EDGE ( 'NONE', *, *, #142024, .F. ) ;
#108059=CARTESIAN_POINT ( 'NONE',  ( 22.49999999999984013, 5.696342897626518464, -7.587980461218345241 ) ) ;
#108060=EDGE_CURVE ( 'NONE', #141725, #61971, #66388, .T. ) ;
#108061=CARTESIAN_POINT ( 'NONE',  ( -23.99451991528749062, 28.92564299267954908, 4.000000000000000000 ) ) ;
#108062=DIRECTION ( 'NONE',  ( 1.000000000000000000, 0.000000000000000000, 0.000000000000000000 ) ) ;
#108063=PLANE ( 'NONE',  #42295 ) ;
#108064=CARTESIAN_POINT ( 'NONE',  ( -32.39513766812459750, 21.75929247661549226, 21.32995629748193878 ) ) ;
#108066=ORIENTED_EDGE ( 'NONE', *, *, #75121, .F. ) ;
#108068=ORIENTED_EDGE ( 'NONE', *, *, #115211, .F. ) ;
#108069=PLANE ( 'NONE',  #29998 ) ;
#108070=CARTESIAN_POINT ( 'NONE',  ( -22.49999999999984723, 16.77039438581777375, 0.4657186855308243500 ) ) ;
#108071=LINE ( 'NONE', #117531, #41771 ) ;
#108072=EDGE_CURVE ( 'NONE', #97559, #25402, #62289, .T. ) ;
#108073=DIRECTION ( 'NONE',  ( -0.000000000000000000, -0.3543493200069152693, 0.9351131265310292928 ) ) ;
#108074=EDGE_LOOP ( 'NONE', ( #80673, #113639, #79878, #104799 ) ) ;
#108075=AXIS2_PLACEMENT_3D ( 'NONE', #20551, #132219, #131486 ) ;
#108077=EDGE_CURVE ( 'NONE', #90471, #7602, #99704, .T. ) ;
#108078=EDGE_LOOP ( 'NONE', ( #26022, #113245, #136861, #5557 ) ) ;
#108079=PLANE ( 'NONE',  #100332 ) ;
#108080=CARTESIAN_POINT ( 'NONE',  ( -34.49999999999976552, 3.054329344830908344, 4.994342998332172101 ) ) ;
#108081=DIRECTION ( 'NONE',  ( -0.7071067811865486830, -0.7071067811865464625, 0.000000000000000000 ) ) ;
#108082=DIRECTION ( 'NONE',  ( -0.7071067811865486830, 0.7071067811865464625, 0.000000000000000000 ) ) ;
#108083=VECTOR ( 'NONE', #10405, 1000.000000000000000 ) ;
#108084=AXIS2_PLACEMENT_3D ( 'NONE', #2169, #49324, #47213 ) ;
#108085=EDGE_CURVE ( 'NONE', #53550, #94406, #117335, .T. ) ;
#108086=EDGE_CURVE ( 'NONE', #135769, #81079, #111287, .T. ) ;
#108089=ORIENTED_EDGE ( 'NONE', *, *, #115502, .T. ) ;
#108090=EDGE_CURVE ( 'NONE', #35748, #63769, #65711, .T. ) ;
#108091=VECTOR ( 'NONE', #43381, 1000.000000000000000 ) ;
#108092=CARTESIAN_POINT ( 'NONE',  ( 45.48921356237309510, -27.52281430457087197, 5.000000000000000000 ) ) ;
#108093=ORIENTED_EDGE ( 'NONE', *, *, #116529, .T. ) ;
#108095=VECTOR ( 'NONE', #114683, 1000.000000000000000 ) ;
#108096=ORIENTED_EDGE ( 'NONE', *, *, #64689, .T. ) ;
#108097=EDGE_CURVE ( 'NONE', #106517, #103136, #43919, .T. ) ;
#108098=FACE_OUTER_BOUND ( 'NONE', #72751, .T. ) ;
#108099=EDGE_LOOP ( 'NONE', ( #111054, #60080, #32420, #122268 ) ) ;
#108100=CARTESIAN_POINT ( 'NONE',  ( -23.99999999999982236, 14.58746187583909837, 4.000000000000000000 ) ) ;
#108101=CARTESIAN_POINT ( 'NONE',  ( -25.49999999999981881, -10.91253812416064761, 4.000000000000000000 ) ) ;
#108102=ADVANCED_FACE ( 'NONE', ( #44669 ), #7866, .T. ) ;
#108103=PLANE ( 'NONE',  #97433 ) ;
#108104=FACE_BOUND ( 'NONE', #81096, .T. ) ;
#108107=FACE_OUTER_BOUND ( 'NONE', #28211, .T. ) ;
#108108=DIRECTION ( 'NONE',  ( 0.000000000000000000, 0.000000000000000000, -1.000000000000000000 ) ) ;
#108109=ORIENTED_EDGE ( 'NONE', *, *, #56944, .T. ) ;
#108110=FACE_OUTER_BOUND ( 'NONE', #41533, .T. ) ;
#108111=ORIENTED_EDGE ( 'NONE', *, *, #69548, .F. ) ;
#108112=VECTOR ( 'NONE', #126527, 1000.000000000000000 ) ;
#108113=EDGE_CURVE ( 'NONE', #18835, #65082, #84735, .T. ) ;
#108114=VERTEX_POINT ( 'NONE', #29620 ) ;
#108115=PLANE ( 'NONE',  #67995 ) ;
#108116=EDGE_LOOP ( 'NONE', ( #133936, #112276, #69201, #73993 ) ) ;
#108118=AXIS2_PLACEMENT_3D ( 'NONE', #108504, #8473, #96916 ) ;
#108119=ORIENTED_EDGE ( 'NONE', *, *, #60039, .F. ) ;
#108120=CARTESIAN_POINT ( 'NONE',  ( -34.42500000000001137, 0.000000000000000000, 0.000000000000000000 ) ) ;
#108121=EDGE_CURVE ( 'NONE', #20507, #103353, #73864, .T. ) ;
#108122=ORIENTED_EDGE ( 'NONE', *, *, #48089, .F. ) ;
#108126=ADVANCED_FACE ( 'NONE', ( #96285 ), #140529, .F. ) ;
#108127=CARTESIAN_POINT ( 'NONE',  ( -69.18398860626899705, 28.73617430169835529, 5.000000000000000000 ) ) ;
#108128=CARTESIAN_POINT ( 'NONE',  ( 2.207106781186530586, -11.24070752338416845, 5.000000000000000000 ) ) ;
#108129=CARTESIAN_POINT ( 'NONE',  ( 25.51290636584444016, -22.22500000000000142, -17.90218200959884953 ) ) ;
#108130=EDGE_CURVE ( 'NONE', #5968, #97631, #3005, .T. ) ;
#108131=DIRECTION ( 'NONE',  ( 0.7071067811865486830, -0.7071067811865464625, -0.000000000000000000 ) ) ;
#108132=LINE ( 'NONE', #10957, #13901 ) ;
#108133=VERTEX_POINT ( 'NONE', #92379 ) ;
#108134=VECTOR ( 'NONE', #123797, 1000.000000000000000 ) ;
#108135=ORIENTED_EDGE ( 'NONE', *, *, #139176, .F. ) ;
#108136=LINE ( 'NONE', #52356, #77490 ) ;
#108137=DIRECTION ( 'NONE',  ( -0.000000000000000000, 0.000000000000000000, 1.000000000000000000 ) ) ;
#108138=ORIENTED_EDGE ( 'NONE', *, *, #110063, .T. ) ;
#108139=EDGE_CURVE ( 'NONE', #109145, #78583, #103267, .T. ) ;
#108140=EDGE_LOOP ( 'NONE', ( #44694, #70430, #79863, #28985 ) ) ;
#108141=ORIENTED_EDGE ( 'NONE', *, *, #111628, .T. ) ;
#108142=CARTESIAN_POINT ( 'NONE',  ( -33.04687264925814816, -22.22500000000000142, 4.288307338716745853 ) ) ;
#108143=CYLINDRICAL_SURFACE ( 'NONE', #3892, 0.5000000000000004441 ) ;
#108144=DIRECTION ( 'NONE',  ( 0.7071067811865487940, 0.7071067811865463515, 0.000000000000000000 ) ) ;
#108145=ORIENTED_EDGE ( 'NONE', *, *, #21804, .T. ) ;
#108146=CARTESIAN_POINT ( 'NONE',  ( -23.99999999999982592, 4.384688058510544550, -7.090945410444739139 ) ) ;
#108148=ORIENTED_EDGE ( 'NONE', *, *, #75523, .F. ) ;
#108150=VECTOR ( 'NONE', #18003, 1000.000000000000000 ) ;
#108152=LINE ( 'NONE', #109611, #69739 ) ;
#108153=DIRECTION ( 'NONE',  ( 0.7071067811865486830, -0.7071067811865464625, -0.000000000000000000 ) ) ;
#108154=FACE_OUTER_BOUND ( 'NONE', #21052, .T. ) ;
#108155=EDGE_LOOP ( 'NONE', ( #133460, #86042, #77562, #50818 ) ) ;
#108157=ORIENTED_EDGE ( 'NONE', *, *, #10527, .F. ) ;
#108160=LINE ( 'NONE', #40810, #51599 ) ;
#108161=DIRECTION ( 'NONE',  ( 0.3543493200069162685, -0.000000000000000000, -0.9351131265310288487 ) ) ;
#108162=ORIENTED_EDGE ( 'NONE', *, *, #87561, .T. ) ;
#108163=AXIS2_PLACEMENT_3D ( 'NONE', #99677, #353, #111261 ) ;
#108164=DIRECTION ( 'NONE',  ( 0.7071067811865487940, 0.7071067811865463515, 0.000000000000000000 ) ) ;
#108165=LINE ( 'NONE', #65448, #39783 ) ;
#108166=VERTEX_POINT ( 'NONE', #56956 ) ;
#108167=CARTESIAN_POINT ( 'NONE',  ( -48.48921356237309510, -27.52281430457089328, 5.000000000000000000 ) ) ;
#108169=ORIENTED_EDGE ( 'NONE', *, *, #20302, .T. ) ;
#108171=AXIS2_PLACEMENT_3D ( 'NONE', #136654, #1130, #45408 ) ;
#108172=DIRECTION ( 'NONE',  ( -0.7071067811865487940, 0.7071067811865463515, 0.000000000000000000 ) ) ;
#108173=VERTEX_POINT ( 'NONE', #101852 ) ;
#108174=ORIENTED_EDGE ( 'NONE', *, *, #57935, .T. ) ;
#108175=DIRECTION ( 'NONE',  ( 0.6830127018922181881, 0.6830127018922202975, -0.2588190451025214056 ) ) ;
#108177=VECTOR ( 'NONE', #142055, 1000.000000000000000 ) ;
#108178=VECTOR ( 'NONE', #129343, 999.9999999999998863 ) ;
#108180=LINE ( 'NONE', #21207, #129233 ) ;
#108181=ADVANCED_FACE ( 'NONE', ( #133776 ), #57669, .F. ) ;
#108182=VECTOR ( 'NONE', #1448, 1000.000000000000000 ) ;
#108183=CARTESIAN_POINT ( 'NONE',  ( -72.29974487139158157, -27.71228299555256669, 4.000000000000000000 ) ) ;
#108184=CARTESIAN_POINT ( 'NONE',  ( 18.18398860626898994, 28.73617430169800002, 5.000000000000000000 ) ) ;
#108185=ORIENTED_EDGE ( 'NONE', *, *, #79973, .F. ) ;
#108186=PLANE ( 'NONE',  #97453 ) ;
#108187=LINE ( 'NONE', #64724, #116109 ) ;
#108188=LINE ( 'NONE', #84370, #23868 ) ;
#108189=VECTOR ( 'NONE', #127359, 1000.000000000000227 ) ;
#108192=CARTESIAN_POINT ( 'NONE',  ( -20.20710678118639692, -20.24070752338406720, 5.000000000000000000 ) ) ;
#108193=VERTEX_POINT ( 'NONE', #78681 ) ;
#108194=CARTESIAN_POINT ( 'NONE',  ( -17.99451991528748351, 28.92564299267950645, 4.000000000000000000 ) ) ;
#108195=ORIENTED_EDGE ( 'NONE', *, *, #100449, .T. ) ;
#108197=CARTESIAN_POINT ( 'NONE',  ( 30.18398860626900060, 28.73617430169808173, 5.000000000000000000 ) ) ;
#108198=PLANE ( 'NONE',  #55563 ) ;
#108199=ORIENTED_EDGE ( 'NONE', *, *, #29855, .F. ) ;
#108201=DIRECTION ( 'NONE',  ( -0.7071067811865487940, 0.7071067811865463515, 0.000000000000000000 ) ) ;
#108202=DIRECTION ( 'NONE',  ( -0.7071067811865486830, -0.7071067811865464625, 0.000000000000000000 ) ) ;
#108203=CARTESIAN_POINT ( 'NONE',  ( -20.67183060077632817, -18.74070752338409207, 4.000000000000000000 ) ) ;
#108204=FACE_OUTER_BOUND ( 'NONE', #97322, .T. ) ;
#108205=VERTEX_POINT ( 'NONE', #3915 ) ;
#108207=LINE ( 'NONE', #8869, #9768 ) ;
#108209=CARTESIAN_POINT ( 'NONE',  ( -31.82816939922330945, 15.75929247661555443, 4.000000000000000000 ) ) ;
#108210=CARTESIAN_POINT ( 'NONE',  ( 13.60343192894634967, -14.24070752338413293, 19.24067776001729158 ) ) ;
#108211=PLANE ( 'NONE',  #137718 ) ;
#108212=CARTESIAN_POINT ( 'NONE',  ( -45.48921356237309510, -27.52281430457087197, 5.000000000000000000 ) ) ;
#108215=VECTOR ( 'NONE', #102877, 1000.000000000000000 ) ;
#108216=LINE ( 'NONE', #131449, #69334 ) ;
#108217=ORIENTED_EDGE ( 'NONE', *, *, #67327, .F. ) ;
#108218=ORIENTED_EDGE ( 'NONE', *, *, #6447, .F. ) ;
#108220=CARTESIAN_POINT ( 'NONE',  ( -21.18398860626899349, 28.73617430169802134, 5.000000000000000000 ) ) ;
#108221=DIRECTION ( 'NONE',  ( 0.7071067811865487940, 0.7071067811865463515, -0.000000000000000000 ) ) ;
#108222=DIRECTION ( 'NONE',  ( -0.000000000000000000, 0.3543493200069153248, 0.9351131265310292928 ) ) ;
#108223=VERTEX_POINT ( 'NONE', #91687 ) ;
#108224=CARTESIAN_POINT ( 'NONE',  ( 1.828169399223519953, -20.24070752338407431, 4.000000000000000000 ) ) ;
#108226=VERTEX_POINT ( 'NONE', #23577 ) ;
#108227=EDGE_CURVE ( 'NONE', #80973, #126820, #70690, .T. ) ;
#108228=LINE ( 'NONE', #84407, #45566 ) ;
#108229=ORIENTED_EDGE ( 'NONE', *, *, #30605, .T. ) ;
#108230=ORIENTED_EDGE ( 'NONE', *, *, #10782, .F. ) ;
#108233=CARTESIAN_POINT ( 'NONE',  ( 12.70612307739187052, 22.22500000000000142, 4.000000000000000000 ) ) ;
#108234=DIRECTION ( 'NONE',  ( -0.7071067811865487940, 0.7071067811865463515, 0.000000000000000000 ) ) ;
#108235=ORIENTED_EDGE ( 'NONE', *, *, #2751, .F. ) ;
#108236=CARTESIAN_POINT ( 'NONE',  ( 12.48921356237309155, -27.52281430457064104, 5.000000000000000000 ) ) ;
#108237=EDGE_CURVE ( 'NONE', #76949, #137069, #25716, .T. ) ;
#108238=EDGE_CURVE ( 'NONE', #20015, #24720, #69989, .T. ) ;
#108242=CARTESIAN_POINT ( 'NONE',  ( -15.56584921360887108, 8.021612662230191759, 4.000000000000000000 ) ) ;
#108244=DIRECTION ( 'NONE',  ( -0.7071067811865486830, -0.7071067811865464625, -0.000000000000000000 ) ) ;
#108245=EDGE_CURVE ( 'NONE', #102633, #52625, #14836, .T. ) ;
#108248=VECTOR ( 'NONE', #73577, 999.9999999999998863 ) ;
#108250=CARTESIAN_POINT ( 'NONE',  ( -4.499999999999962697, 16.46639925780210234, 5.000000000000000000 ) ) ;
#108251=EDGE_CURVE ( 'NONE', #35225, #142584, #81564, .T. ) ;
#108252=FACE_OUTER_BOUND ( 'NONE', #133072, .T. ) ;
#108253=ORIENTED_EDGE ( 'NONE', *, *, #42871, .F. ) ;
#108254=ORIENTED_EDGE ( 'NONE', *, *, #105264, .T. ) ;
#108255=EDGE_CURVE ( 'NONE', #66262, #66281, #35201, .T. ) ;
#108256=CARTESIAN_POINT ( 'NONE',  ( 11.58838509405160089, 22.22500000000000497, 4.777194822843814137 ) ) ;
#108258=ORIENTED_EDGE ( 'NONE', *, *, #125170, .F. ) ;
#108259=EDGE_CURVE ( 'NONE', #132937, #75865, #123640, .T. ) ;
#108260=ORIENTED_EDGE ( 'NONE', *, *, #24807, .T. ) ;
#108261=CARTESIAN_POINT ( 'NONE',  ( -21.32816939922338051, 17.25929247661554911, 4.000000000000000000 ) ) ;
#108262=VERTEX_POINT ( 'NONE', #2509 ) ;
#108264=DIRECTION ( 'NONE',  ( -0.6830127018922180770, -0.6830127018922204085, -0.2588190451025213501 ) ) ;
#108265=VECTOR ( 'NONE', #17763, 1000.000000000000000 ) ;
#108266=EDGE_CURVE ( 'NONE', #91948, #67296, #24295, .T. ) ;
#108267=DIRECTION ( 'NONE',  ( 0.7071067811865487940, 0.7071067811865463515, 0.000000000000000000 ) ) ;
#108268=VECTOR ( 'NONE', #64104, 1000.000000000000000 ) ;
#108269=FACE_BOUND ( 'NONE', #50197, .T. ) ;
#108270=DIRECTION ( 'NONE',  ( 0.7071067811865487940, -0.7071067811865463515, 0.000000000000000000 ) ) ;
#108272=DIRECTION ( 'NONE',  ( -0.7071067811865486830, -0.7071067811865463515, 0.000000000000000000 ) ) ;
#108273=DIRECTION ( 'NONE',  ( -0.7071067811865486830, 0.7071067811865464625, 0.000000000000000000 ) ) ;
#108274=ORIENTED_EDGE ( 'NONE', *, *, #96800, .T. ) ;
#108275=EDGE_CURVE ( 'NONE', #34581, #78703, #80137, .T. ) ;
#108277=AXIS2_PLACEMENT_3D ( 'NONE', #36999, #124730, #37744 ) ;
#108278=LINE ( 'NONE', #19171, #11557 ) ;
#108279=ORIENTED_EDGE ( 'NONE', *, *, #121359, .T. ) ;
#108280=ORIENTED_EDGE ( 'NONE', *, *, #16284, .F. ) ;
#108282=ORIENTED_EDGE ( 'NONE', *, *, #89087, .T. ) ;
#108283=LINE ( 'NONE', #130090, #36022 ) ;
#108284=CARTESIAN_POINT ( 'NONE',  ( -39.29974487139159578, -27.71228299555233576, 4.000000000000000000 ) ) ;
#108285=EDGE_CURVE ( 'NONE', #20535, #105827, #58407, .T. ) ;
#108288=CARTESIAN_POINT ( 'NONE',  ( 8.878526836628477525, -20.24070752338407431, 7.412974875817769593 ) ) ;
#108289=EDGE_CURVE ( 'NONE', #117114, #2861, #84411, .T. ) ;
#108290=LINE ( 'NONE', #75023, #110851 ) ;
#108291=CARTESIAN_POINT ( 'NONE',  ( -21.29974487139158512, -27.71228299555221142, 4.000000000000000000 ) ) ;
#108292=LINE ( 'NONE', #140950, #31922 ) ;
#108293=PLANE ( 'NONE',  #121378 ) ;
#108294=EDGE_CURVE ( 'NONE', #135854, #80606, #60527, .T. ) ;
#108295=DIRECTION ( 'NONE',  ( 0.7071067811865487940, 0.7071067811865463515, -0.000000000000000000 ) ) ;
#108296=LINE ( 'NONE', #8967, #13787 ) ;
#108298=DIRECTION ( 'NONE',  ( -0.000000000000000000, -0.3543493200069152693, 0.9351131265310292928 ) ) ;
#108299=VERTEX_POINT ( 'NONE', #106835 ) ;
#108301=EDGE_CURVE ( 'NONE', #1370, #61259, #106098, .T. ) ;
#108302=DIRECTION ( 'NONE',  ( 0.7071067811865487940, -0.7071067811865463515, 0.000000000000000000 ) ) ;
#108304=VERTEX_POINT ( 'NONE', #39474 ) ;
#108305=VERTEX_POINT ( 'NONE', #139520 ) ;
#108306=CARTESIAN_POINT ( 'NONE',  ( 14.51078643762690490, -27.52281430457045275, 5.000000000000000000 ) ) ;
#108310=DIRECTION ( 'NONE',  ( 0.6830127018922181881, 0.6830127018922202975, -0.2588190451025214056 ) ) ;
#108313=EDGE_LOOP ( 'NONE', ( #68027, #142443, #57919, #110895 ) ) ;
#108315=CARTESIAN_POINT ( 'NONE',  ( -60.48921356237309510, -27.52281430457097500, 5.000000000000000000 ) ) ;
#108316=VERTEX_POINT ( 'NONE', #117005 ) ;
#108318=LINE ( 'NONE', #88042, #128522 ) ;
#108319=CARTESIAN_POINT ( 'NONE',  ( 1.499999999999994449, 0.4497235411627456547, -5.599840258123537140 ) ) ;
#108320=ORIENTED_EDGE ( 'NONE', *, *, #23589, .T. ) ;
#108322=CARTESIAN_POINT ( 'NONE',  ( -23.89661266223020419, -0.3091507863911187037, 4.000000000000000000 ) ) ;
#108324=CARTESIAN_POINT ( 'NONE',  ( 23.29289321881329755, -15.74070752338412049, 5.000000000000000000 ) ) ;
#108326=DIRECTION ( 'NONE',  ( -0.7071067811865486830, -0.7071067811865464625, 0.000000000000000000 ) ) ;
#108327=ORIENTED_EDGE ( 'NONE', *, *, #75130, .T. ) ;
#108330=EDGE_CURVE ( 'NONE', #24720, #111950, #74229, .T. ) ;
#108331=ORIENTED_EDGE ( 'NONE', *, *, #102129, .F. ) ;
#108332=CARTESIAN_POINT ( 'NONE',  ( -20.51078643762690490, -27.52281430457041012, 5.000000000000000000 ) ) ;
#108333=CARTESIAN_POINT ( 'NONE',  ( 39.48921356237310221, -27.52281430457082934, 5.000000000000000000 ) ) ;
#108334=LINE ( 'NONE', #126043, #42182 ) ;
#108335=DIRECTION ( 'NONE',  ( 0.7071067811865487940, 0.7071067811865463515, 0.000000000000000000 ) ) ;
#108336=EDGE_CURVE ( 'NONE', #109228, #140721, #82966, .T. ) ;
#108337=CARTESIAN_POINT ( 'NONE',  ( -3.792893218813421008, -5.240707523384228850, 5.000000000000000000 ) ) ;
#108338=VERTEX_POINT ( 'NONE', #17673 ) ;
#108339=FACE_OUTER_BOUND ( 'NONE', #17524, .T. ) ;
#108340=EDGE_CURVE ( 'NONE', #94913, #59092, #18375, .T. ) ;
#108341=ORIENTED_EDGE ( 'NONE', *, *, #81689, .T. ) ;
#108342=DIRECTION ( 'NONE',  ( -0.7071067811865486830, -0.7071067811865464625, -0.000000000000000000 ) ) ;
#108343=LINE ( 'NONE', #9018, #55170 ) ;
#108344=ORIENTED_EDGE ( 'NONE', *, *, #34201, .T. ) ;
#108345=DIRECTION ( 'NONE',  ( 0.7071067811865487940, 0.7071067811865463515, -0.000000000000000000 ) ) ;
#108346=DIRECTION ( 'NONE',  ( 0.7071067811865486830, -0.7071067811865464625, -0.000000000000000000 ) ) ;
#108347=EDGE_LOOP ( 'NONE', ( #43568, #118727, #101434, #124052 ) ) ;
#108348=ORIENTED_EDGE ( 'NONE', *, *, #114506, .T. ) ;
#108350=CARTESIAN_POINT ( 'NONE',  ( -1.828169399223515512, -20.24070752338407431, 4.000000000000000000 ) ) ;
#108351=DIRECTION ( 'NONE',  ( 1.000000000000000000, 0.000000000000000000, 0.000000000000000000 ) ) ;
#108353=DIRECTION ( 'NONE',  ( 0.7071067811865487940, -0.7071067811865463515, 0.000000000000000000 ) ) ;
#108355=EDGE_CURVE ( 'NONE', #3249, #49064, #61263, .T. ) ;
#108356=FACE_OUTER_BOUND ( 'NONE', #8062, .T. ) ;
#108357=CARTESIAN_POINT ( 'NONE',  ( 0.000000000000000000, 0.000000000000000000, 5.000000000000000000 ) ) ;
#108358=ADVANCED_FACE ( 'NONE', ( #49652 ), #115541, .F. ) ;
#108359=CARTESIAN_POINT ( 'NONE',  ( -57.18398860626899705, 28.73617430169827358, 5.000000000000000000 ) ) ;
#108360=CARTESIAN_POINT ( 'NONE',  ( 34.49999999999976552, 19.39370406404970026, 1.459788787078122319 ) ) ;
#108361=ORIENTED_EDGE ( 'NONE', *, *, #78418, .F. ) ;
#108362=CARTESIAN_POINT ( 'NONE',  ( 17.99999999999986855, -5.527737879153178824, -7.983877177622413335 ) ) ;
#108363=VERTEX_POINT ( 'NONE', #93830 ) ;
#108364=LINE ( 'NONE', #87385, #131147 ) ;
#108365=DIRECTION ( 'NONE',  ( 0.7071067811865487940, 0.7071067811865463515, -0.000000000000000000 ) ) ;
#108366=ORIENTED_EDGE ( 'NONE', *, *, #43197, .F. ) ;
#108367=DIRECTION ( 'NONE',  ( -0.000000000000000000, -0.3543493200069152693, 0.9351131265310292928 ) ) ;
#108368=CARTESIAN_POINT ( 'NONE',  ( 3.183988606268992161, 28.73617430169789699, 5.000000000000000000 ) ) ;
#108369=VERTEX_POINT ( 'NONE', #138057 ) ;
#108370=AXIS2_PLACEMENT_3D ( 'NONE', #3950, #81596, #123678 ) ;
#108371=DIRECTION ( 'NONE',  ( -0.6830127018922180770, -0.6830127018922204085, -0.2588190451025213501 ) ) ;
#108373=DIRECTION ( 'NONE',  ( -0.000000000000000000, -0.3543493200069152693, 0.9351131265310292928 ) ) ;
#108374=CARTESIAN_POINT ( 'NONE',  ( -9.792893218813384593, -17.24070752338409918, 5.000000000000000000 ) ) ;
#108375=ORIENTED_EDGE ( 'NONE', *, *, #20728, .T. ) ;
#108377=DIRECTION ( 'NONE',  ( -0.7071067811865487940, 0.7071067811865463515, 0.000000000000000000 ) ) ;
#108378=LINE ( 'NONE', #109130, #65278 ) ;
#108380=VECTOR ( 'NONE', #23828, 1000.000000000000000 ) ;
#108381=LINE ( 'NONE', #7668, #56914 ) ;
#108383=PLANE ( 'NONE',  #104140 ) ;
#108386=CARTESIAN_POINT ( 'NONE',  ( -29.67183060077625711, -0.7407075233842770334, 4.000000000000000000 ) ) ;
#108387=PLANE ( 'NONE',  #29889 ) ;
#108388=CARTESIAN_POINT ( 'NONE',  ( 13.71003237941630104, 5.842153316012715258, 5.000000000000000000 ) ) ;
#108390=EDGE_LOOP ( 'NONE', ( #44859, #122421, #138497, #85675 ) ) ;
#108391=LINE ( 'NONE', #9076, #74578 ) ;
#108392=VERTEX_POINT ( 'NONE', #11068 ) ;
#108393=AXIS2_PLACEMENT_3D ( 'NONE', #28901, #73137, #62253 ) ;
#108395=DIRECTION ( 'NONE',  ( 0.7071067811865487940, -0.7071067811865463515, 0.000000000000000000 ) ) ;
#108396=CARTESIAN_POINT ( 'NONE',  ( 0.000000000000000000, 21.72500000000000142, 4.500000000000000888 ) ) ;
#108397=VECTOR ( 'NONE', #66368, 1000.000000000000000 ) ;
#108398=ORIENTED_EDGE ( 'NONE', *, *, #73880, .F. ) ;
#108399=CARTESIAN_POINT ( 'NONE',  ( -20.99999999999984368, -3.033600742197705369, 5.000000000000000000 ) ) ;
#108400=( BOUNDED_CURVE ( )  B_SPLINE_CURVE ( 3, ( #118220, #18927, #84226, #64582 ),
 .UNSPECIFIED., .F., .T. ) 
 B_SPLINE_CURVE_WITH_KNOTS ( ( 4, 4 ),
 ( 5.043186909253408956, 5.074607125596347856 ),
 .UNSPECIFIED. ) 
 CURVE ( )  GEOMETRIC_REPRESENTATION_ITEM ( )  RATIONAL_B_SPLINE_CURVE ( ( 1.000000000000000000, 0.9999177325257868620, 0.9999177325257868620, 1.000000000000000000 ) ) 
 REPRESENTATION_ITEM ( '' )  );
#108402=DIRECTION ( 'NONE',  ( -0.6830127018922181881, 0.6830127018922202975, -0.2588190451025214056 ) ) ;
#108403=VECTOR ( 'NONE', #121700, 1000.000000000000000 ) ;
#108405=DIRECTION ( 'NONE',  ( -0.7071067811865486830, -0.7071067811865464625, -0.000000000000000000 ) ) ;
#108406=ADVANCED_FACE ( 'NONE', ( #132925 ), #22655, .F. ) ;
#108407=DIRECTION ( 'NONE',  ( -0.7071067811865486830, -0.7071067811865464625, -0.000000000000000000 ) ) ;
#108408=ORIENTED_EDGE ( 'NONE', *, *, #103550, .F. ) ;
#108409=CARTESIAN_POINT ( 'NONE',  ( 24.18398860626899705, 28.73617430169804265, 5.000000000000000000 ) ) ;
#108410=LINE ( 'NONE', #73691, #119372 ) ;
#108411=DIRECTION ( 'NONE',  ( 0.7071067811865486830, -0.7071067811865464625, -0.000000000000000000 ) ) ;
#108412=CARTESIAN_POINT ( 'NONE',  ( 15.79289321881333841, 12.75929247661558463, 5.000000000000000000 ) ) ;
#108413=ORIENTED_EDGE ( 'NONE', *, *, #32929, .F. ) ;
#108414=EDGE_CURVE ( 'NONE', #59299, #61284, #32895, .T. ) ;
#108415=VERTEX_POINT ( 'NONE', #119833 ) ;
#108416=EDGE_CURVE ( 'NONE', #109375, #53162, #77114, .T. ) ;
#108419=EDGE_CURVE ( 'NONE', #2143, #122205, #141635, .T. ) ;
#108420=DIRECTION ( 'NONE',  ( -0.000000000000000000, -0.3543493200069152693, 0.9351131265310292928 ) ) ;
#108421=CARTESIAN_POINT ( 'NONE',  ( -18.70701326429291456, -21.74070752338405654, 4.999753212805221558 ) ) ;
#108424=ORIENTED_EDGE ( 'NONE', *, *, #70383, .F. ) ;
#108425=AXIS2_PLACEMENT_3D ( 'NONE', #55770, #132636, #143459 ) ;
#108426=EDGE_CURVE ( 'NONE', #24049, #119425, #64786, .T. ) ;
#108428=CARTESIAN_POINT ( 'NONE',  ( 21.70701326429288613, -21.74070752338406365, 4.999753212805217117 ) ) ;
#108430=EDGE_LOOP ( 'NONE', ( #138200, #31934, #57243, #98017 ) ) ;
#108431=EDGE_CURVE ( 'NONE', #35909, #40105, #52454, .T. ) ;
#108432=CARTESIAN_POINT ( 'NONE',  ( 16.49999999999988987, 13.56627193232216477, -10.57019076586064976 ) ) ;
#108433=CARTESIAN_POINT ( 'NONE',  ( 0.000000000000000000, 0.000000000000000000, 5.000000000000000000 ) ) ;
#108434=CARTESIAN_POINT ( 'NONE',  ( -39.48921356237310221, -27.52281430457082934, 5.000000000000000000 ) ) ;
#108436=EDGE_LOOP ( 'NONE', ( #15, #110160, #29118, #111027 ) ) ;
#108437=EDGE_CURVE ( 'NONE', #37549, #49848, #96644, .T. ) ;
#108438=EDGE_CURVE ( 'NONE', #115267, #28809, #85802, .T. ) ;
#108439=CARTESIAN_POINT ( 'NONE',  ( 11.70025512860841133, -27.71228299555198049, 4.000000000000000000 ) ) ;
#108440=CARTESIAN_POINT ( 'NONE',  ( 13.49999999999991118, 12.43112307739206024, 4.000000000000000000 ) ) ;
#108444=EDGE_CURVE ( 'NONE', #45259, #20400, #130773, .T. ) ;
#108447=ORIENTED_EDGE ( 'NONE', *, *, #140266, .T. ) ;
#108450=ORIENTED_EDGE ( 'NONE', *, *, #106279, .T. ) ;
#108451=ORIENTED_EDGE ( 'NONE', *, *, #121376, .T. ) ;
#108452=CARTESIAN_POINT ( 'NONE',  ( 32.99999999999977263, -11.35517001088068945, -1.126524801160033507 ) ) ;
#108453=CARTESIAN_POINT ( 'NONE',  ( 15.79333936457837062, 21.75929247661549937, 4.998822639870715179 ) ) ;
#108454=CARTESIAN_POINT ( 'NONE',  ( 13.31312592467349454, 1.515602562757560223, 4.636692559446319528 ) ) ;
#108455=VERTEX_POINT ( 'NONE', #53931 ) ;
#108456=PLANE ( 'NONE',  #66814 ) ;
#108457=LINE ( 'NONE', #140416, #79673 ) ;
#108459=DIRECTION ( 'NONE',  ( -0.6830127018922180770, -0.6830127018922204085, -0.2588190451025213501 ) ) ;
#108460=EDGE_CURVE ( 'NONE', #14564, #48060, #33604, .T. ) ;
#108462=AXIS2_PLACEMENT_3D ( 'NONE', #104929, #70224, #15053 ) ;
#108463=AXIS2_PLACEMENT_3D ( 'NONE', #75245, #109269, #142622 ) ;
#108464=FACE_OUTER_BOUND ( 'NONE', #45289, .T. ) ;
#108465=AXIS2_PLACEMENT_3D ( 'NONE', #5036, #27526, #137025 ) ;
#108466=ORIENTED_EDGE ( 'NONE', *, *, #72526, .T. ) ;
#108467=FACE_OUTER_BOUND ( 'NONE', #112886, .T. ) ;
#108469=VECTOR ( 'NONE', #114546, 999.9999999999998863 ) ;
#108470=EDGE_LOOP ( 'NONE', ( #121947, #59970, #18808, #93793 ) ) ;
#108471=DIRECTION ( 'NONE',  ( -0.3543493200069162685, -0.000000000000000000, -0.9351131265310288487 ) ) ;
#108473=ORIENTED_EDGE ( 'NONE', *, *, #73214, .F. ) ;
#108474=VERTEX_POINT ( 'NONE', #43040 ) ;
#108476=AXIS2_PLACEMENT_3D ( 'NONE', #77695, #45097, #76999 ) ;
#108477=ORIENTED_EDGE ( 'NONE', *, *, #30210, .T. ) ;
#108478=ORIENTED_EDGE ( 'NONE', *, *, #128501, .T. ) ;
#108479=VECTOR ( 'NONE', #38979, 1000.000000000000000 ) ;
#108480=EDGE_CURVE ( 'NONE', #90561, #42516, #32677, .T. ) ;
#108481=CARTESIAN_POINT ( 'NONE',  ( 15.18398860626900237, 28.73617430169797871, 5.000000000000000000 ) ) ;
#108484=EDGE_CURVE ( 'NONE', #136079, #93121, #21272, .T. ) ;
#108486=ORIENTED_EDGE ( 'NONE', *, *, #141566, .T. ) ;
#108487=DIRECTION ( 'NONE',  ( -0.6830127018922180770, -0.6830127018922204085, -0.2588190451025213501 ) ) ;
#108489=FACE_OUTER_BOUND ( 'NONE', #124912, .T. ) ;
#108492=ORIENTED_EDGE ( 'NONE', *, *, #22995, .T. ) ;
#108493=LINE ( 'NONE', #9176, #124764 ) ;
#108494=EDGE_CURVE ( 'NONE', #32917, #67920, #89383, .T. ) ;
#108495=ORIENTED_EDGE ( 'NONE', *, *, #45865, .T. ) ;
#108496=ORIENTED_EDGE ( 'NONE', *, *, #10758, .F. ) ;
#108497=ORIENTED_EDGE ( 'NONE', *, *, #129858, .T. ) ;
#108499=VECTOR ( 'NONE', #141399, 1000.000000000000000 ) ;
#108500=ORIENTED_EDGE ( 'NONE', *, *, #55169, .T. ) ;
#108501=VECTOR ( 'NONE', #36764, 1000.000000000000000 ) ;
#108502=VECTOR ( 'NONE', #53496, 999.9999999999998863 ) ;
#108503=DIRECTION ( 'NONE',  ( 1.000000000000000000, 0.000000000000000000, 0.000000000000000000 ) ) ;
#108504=CARTESIAN_POINT ( 'NONE',  ( 51.18398860626899705, 28.73617430169823095, 5.000000000000000000 ) ) ;
#108505=VECTOR ( 'NONE', #91805, 1000.000000000000000 ) ;
#108506=ADVANCED_FACE ( 'NONE', ( #56802 ), #45901, .F. ) ;
#108508=EDGE_LOOP ( 'NONE', ( #59064, #24764, #49787, #14261, #139018 ) ) ;
#108509=CARTESIAN_POINT ( 'NONE',  ( -6.489213562373093325, -27.52281430457059841, 5.000000000000000000 ) ) ;
#108510=ORIENTED_EDGE ( 'NONE', *, *, #134560, .T. ) ;
#108512=AXIS2_PLACEMENT_3D ( 'NONE', #54355, #10087, #76073 ) ;
#108515=DIRECTION ( 'NONE',  ( 0.6830127018922181881, 0.6830127018922202975, -0.2588190451025214056 ) ) ;
#108516=CARTESIAN_POINT ( 'NONE',  ( 0.000000000000000000, -13.97847968911260530, -0.1324546996126791387 ) ) ;
#108518=EDGE_LOOP ( 'NONE', ( #97844, #31835, #100803, #60904 ) ) ;
#108519=VERTEX_POINT ( 'NONE', #113260 ) ;
#108520=CARTESIAN_POINT ( 'NONE',  ( -51.18398860626899705, 28.73617430169823095, 5.000000000000000000 ) ) ;
#108521=FACE_OUTER_BOUND ( 'NONE', #41576, .T. ) ;
#108523=LINE ( 'NONE', #74536, #137617 ) ;
#108524=CARTESIAN_POINT ( 'NONE',  ( 57.18398860626899705, 28.73617430169827358, 5.000000000000000000 ) ) ;
#108525=EDGE_CURVE ( 'NONE', #43020, #15065, #48044, .T. ) ;
#108526=CARTESIAN_POINT ( 'NONE',  ( 34.49999999999975842, 8.900465351122182511, -2.516491619111592914 ) ) ;
#108527=LINE ( 'NONE', #131763, #138684 ) ;
#108532=ORIENTED_EDGE ( 'NONE', *, *, #38155, .T. ) ;
#108533=CARTESIAN_POINT ( 'NONE',  ( -15.18398860626900237, 28.73617430169797871, 5.000000000000000000 ) ) ;
#108534=ORIENTED_EDGE ( 'NONE', *, *, #55691, .T. ) ;
#108535=FACE_OUTER_BOUND ( 'NONE', #41216, .T. ) ;
#108536=VERTEX_POINT ( 'NONE', #111103 ) ;
#108537=CARTESIAN_POINT ( 'NONE',  ( 22.99806943317885199, -22.22500000000000142, 4.500000000000000888 ) ) ;
#108539=EDGE_LOOP ( 'NONE', ( #15391, #3422, #62122 ) ) ;
#108540=ADVANCED_FACE ( 'NONE', ( #78514 ), #56081, .F. ) ;
#108541=DIRECTION ( 'NONE',  ( 0.7071067811865486830, -0.7071067811865464625, -0.000000000000000000 ) ) ;
#108542=ORIENTED_EDGE ( 'NONE', *, *, #103549, .F. ) ;
#108545=CARTESIAN_POINT ( 'NONE',  ( 34.92499999999998295, 3.662461875838979974, 4.000000000000000000 ) ) ;
#108548=LINE ( 'NONE', #53507, #100765 ) ;
#108550=LINE ( 'NONE', #96958, #67036 ) ;
#108551=CARTESIAN_POINT ( 'NONE',  ( -13.49999999999990052, 5.696342897626497148, -7.587980461218431394 ) ) ;
#108552=CARTESIAN_POINT ( 'NONE',  ( 20.99999999999986500, -10.44781430457071458, 5.000000000000000000 ) ) ;
#108553=CARTESIAN_POINT ( 'NONE',  ( 20.99999999999987210, 20.58746187583903264, 4.000000000000000000 ) ) ;
#108554=LINE ( 'NONE', #9234, #2135 ) ;
#108558=DIRECTION ( 'NONE',  ( 0.6830127018922180770, -0.6830127018922204085, -0.2588190451025213501 ) ) ;
#108559=ORIENTED_EDGE ( 'NONE', *, *, #137198, .T. ) ;
#108560=EDGE_CURVE ( 'NONE', #40356, #5851, #58239, .T. ) ;
#108562=DIRECTION ( 'NONE',  ( 0.6830127018922180770, -0.6830127018922204085, -0.2588190451025213501 ) ) ;
#108563=ORIENTED_EDGE ( 'NONE', *, *, #115619, .T. ) ;
#108564=PLANE ( 'NONE',  #50334 ) ;
#108565=DIRECTION ( 'NONE',  ( -0.000000000000000000, -0.3543493200069152693, 0.9351131265310292928 ) ) ;
#108566=AXIS2_PLACEMENT_3D ( 'NONE', #121824, #131300, #66765 ) ;
#108568=EDGE_LOOP ( 'NONE', ( #21709, #5835, #16245, #60806 ) ) ;
#108570=VECTOR ( 'NONE', #24247, 1000.000000000000114 ) ;
#108572=LINE ( 'NONE', #131089, #116888 ) ;
#108573=DIRECTION ( 'NONE',  ( 0.000000000000000000, 0.000000000000000000, 1.000000000000000000 ) ) ;
#108577=DIRECTION ( 'NONE',  ( -0.6830127018922181881, 0.6830127018922202975, -0.2588190451025214056 ) ) ;
#108578=ORIENTED_EDGE ( 'NONE', *, *, #55144, .T. ) ;
#108580=DIRECTION ( 'NONE',  ( 0.7071067811865486830, -0.7071067811865464625, -0.000000000000000000 ) ) ;
#108581=PLANE ( 'NONE',  #47933 ) ;
#108582=AXIS2_PLACEMENT_3D ( 'NONE', #41520, #121926, #54576 ) ;
#108583=( BOUNDED_CURVE ( )  B_SPLINE_CURVE ( 3, ( #18025, #61609, #19492, #139876 ),
 .UNSPECIFIED., .F., .T. ) 
 B_SPLINE_CURVE_WITH_KNOTS ( ( 4, 4 ),
 ( 5.043186909253412509, 5.074607125596351409 ),
 .UNSPECIFIED. ) 
 CURVE ( )  GEOMETRIC_REPRESENTATION_ITEM ( )  RATIONAL_B_SPLINE_CURVE ( ( 1.000000000000000000, 0.9999177325257868620, 0.9999177325257868620, 1.000000000000000000 ) ) 
 REPRESENTATION_ITEM ( '' )  );
#108584=DIRECTION ( 'NONE',  ( -0.000000000000000000, 0.3543493200069153248, 0.9351131265310292928 ) ) ;
#108585=ORIENTED_EDGE ( 'NONE', *, *, #68544, .T. ) ;
#108587=VERTEX_POINT ( 'NONE', #124868 ) ;
#108588=EDGE_CURVE ( 'NONE', #98608, #6354, #47370, .T. ) ;
#108590=ORIENTED_EDGE ( 'NONE', *, *, #123370, .T. ) ;
#108591=EDGE_CURVE ( 'NONE', #17366, #74602, #23396, .T. ) ;
#108593=EDGE_CURVE ( 'NONE', #110860, #140411, #45205, .T. ) ;
#108594=VECTOR ( 'NONE', #51737, 1000.000000000000000 ) ;
#108595=VECTOR ( 'NONE', #66910, 1000.000000000000000 ) ;
#108596=PLANE ( 'NONE',  #142987 ) ;
#108598=EDGE_CURVE ( 'NONE', #43430, #42382, #102431, .T. ) ;
#108599=CARTESIAN_POINT ( 'NONE',  ( 9.489213562373095101, -27.52281430457062328, 5.000000000000000000 ) ) ;
#108600=LINE ( 'NONE', #33274, #132236 ) ;
#108601=VECTOR ( 'NONE', #168, 1000.000000000000000 ) ;
#108603=ORIENTED_EDGE ( 'NONE', *, *, #80924, .T. ) ;
#108604=CARTESIAN_POINT ( 'NONE',  ( 9.183988606268997046, 28.73617430169793607, 5.000000000000000000 ) ) ;
#108605=DIRECTION ( 'NONE',  ( 0.3543493200069162685, -0.000000000000000000, -0.9351131265310288487 ) ) ;
#108607=VECTOR ( 'NONE', #133097, 1000.000000000000000 ) ;
#108608=FACE_OUTER_BOUND ( 'NONE', #98633, .T. ) ;
#108609=VECTOR ( 'NONE', #72975, 1000.000000000000000 ) ;
#108611=ORIENTED_EDGE ( 'NONE', *, *, #23716, .F. ) ;
#108612=EDGE_LOOP ( 'NONE', ( #138149, #67621, #12713, #132945 ) ) ;
#108613=EDGE_CURVE ( 'NONE', #65412, #52532, #133615, .T. ) ;
#108614=EDGE_LOOP ( 'NONE', ( #20698, #29039, #102631, #132906 ) ) ;
#108615=CARTESIAN_POINT ( 'NONE',  ( 6.183988606268994381, 28.73617430169791476, 5.000000000000000000 ) ) ;
#108617=DIRECTION ( 'NONE',  ( -0.7071067811865486830, 0.7071067811865464625, 0.000000000000000000 ) ) ;
#108620=AXIS2_PLACEMENT_3D ( 'NONE', #93933, #138170, #62054 ) ;
#108621=DIRECTION ( 'NONE',  ( -0.000000000000000000, 0.3543493200069153248, 0.9351131265310292928 ) ) ;
#108622=EDGE_CURVE ( 'NONE', #28852, #45152, #90082, .T. ) ;
#108623=LINE ( 'NONE', #10743, #138 ) ;
#108625=ORIENTED_EDGE ( 'NONE', *, *, #101118, .F. ) ;
#108626=ORIENTED_EDGE ( 'NONE', *, *, #58246, .F. ) ;
#108627=DIRECTION ( 'NONE',  ( -0.7071067811865486830, -0.7071067811865464625, 0.000000000000000000 ) ) ;
#108628=VERTEX_POINT ( 'NONE', #35761 ) ;
#108629=ORIENTED_EDGE ( 'NONE', *, *, #81230, .F. ) ;
#108630=EDGE_CURVE ( 'NONE', #80972, #92701, #35030, .T. ) ;
#108631=VECTOR ( 'NONE', #107491, 1000.000000000000227 ) ;
#108632=DIRECTION ( 'NONE',  ( 1.000000000000000000, 0.000000000000000000, 0.000000000000000000 ) ) ;
#108633=CARTESIAN_POINT ( 'NONE',  ( 30.32816939922331656, -15.74070752338412760, 4.000000000000000000 ) ) ;
#108635=CARTESIAN_POINT ( 'NONE',  ( -19.63753812416085154, 22.22500000000000142, 4.000000000000000000 ) ) ;
#108636=CARTESIAN_POINT ( 'NONE',  ( -0.3281693992235254487, -9.740707523384187994, 4.000000000000000000 ) ) ;
#108637=EDGE_CURVE ( 'NONE', #21299, #118847, #80669, .T. ) ;
#108639=DIRECTION ( 'NONE',  ( 0.3543493200069162685, -0.000000000000000000, -0.9351131265310288487 ) ) ;
#108640=ORIENTED_EDGE ( 'NONE', *, *, #65192, .T. ) ;
#108644=LINE ( 'NONE', #9324, #108177 ) ;
#108645=ORIENTED_EDGE ( 'NONE', *, *, #11872, .F. ) ;
#108647=ORIENTED_EDGE ( 'NONE', *, *, #134458, .F. ) ;
#108648=LINE ( 'NONE', #109400, #62090 ) ;
#108649=VERTEX_POINT ( 'NONE', #69816 ) ;
#108650=EDGE_LOOP ( 'NONE', ( #43941, #98154, #11400, #9290 ) ) ;
#108651=ORIENTED_EDGE ( 'NONE', *, *, #62664, .F. ) ;
#108654=DIRECTION ( 'NONE',  ( -0.7071067811865486830, 0.7071067811865464625, 0.000000000000000000 ) ) ;
#108655=FACE_OUTER_BOUND ( 'NONE', #105179, .T. ) ;
#108656=DIRECTION ( 'NONE',  ( -0.7071067811865486830, -0.7071067811865464625, 0.000000000000000000 ) ) ;
#108657=DIRECTION ( 'NONE',  ( -0.7071067811865487940, 0.7071067811865463515, -0.000000000000000000 ) ) ;
#108658=DIRECTION ( 'NONE',  ( -0.000000000000000000, 0.3543493200069153248, 0.9351131265310292928 ) ) ;
#108659=LINE ( 'NONE', #97062, #117721 ) ;
#108660=CARTESIAN_POINT ( 'NONE',  ( 39.29974487139159578, -27.71228299555233576, 4.000000000000000000 ) ) ;
#108662=EDGE_CURVE ( 'NONE', #133807, #114819, #139350, .T. ) ;
#108663=ORIENTED_EDGE ( 'NONE', *, *, #23700, .T. ) ;
#108664=VERTEX_POINT ( 'NONE', #70541 ) ;
#108665=AXIS2_PLACEMENT_3D ( 'NONE', #65565, #33635, #56110 ) ;
#108666=EDGE_LOOP ( 'NONE', ( #138156, #97490, #87299, #52065 ) ) ;
#108667=EDGE_LOOP ( 'NONE', ( #43340, #31235, #34706, #6990 ) ) ;
#108668=LINE ( 'NONE', #95687, #88911 ) ;
#108669=AXIS2_PLACEMENT_3D ( 'NONE', #40603, #84806, #16683 ) ;
#108670=VECTOR ( 'NONE', #132129, 1000.000000000000000 ) ;
#108671=VERTEX_POINT ( 'NONE', #137902 ) ;
#108673=VECTOR ( 'NONE', #49156, 1000.000000000000000 ) ;
#108674=VERTEX_POINT ( 'NONE', #83528 ) ;
#108675=DIRECTION ( 'NONE',  ( -0.7071067811865487940, 0.7071067811865463515, 0.000000000000000000 ) ) ;
#108676=DIRECTION ( 'NONE',  ( 0.6830127018922181881, 0.6830127018922202975, -0.2588190451025214056 ) ) ;
#108677=ADVANCED_FACE ( 'NONE', ( #106657 ), #72686, .F. ) ;
#108679=ORIENTED_EDGE ( 'NONE', *, *, #6811, .F. ) ;
#108680=LINE ( 'NONE', #8643, #20908 ) ;
#108681=AXIS2_PLACEMENT_3D ( 'NONE', #139097, #15137, #126758 ) ;
#108682=VERTEX_POINT ( 'NONE', #105940 ) ;
#108683=DIRECTION ( 'NONE',  ( -0.000000000000000000, 0.3543493200069153248, 0.9351131265310292928 ) ) ;
#108684=DIRECTION ( 'NONE',  ( -0.000000000000000000, 0.000000000000000000, 1.000000000000000000 ) ) ;
#108686=AXIS2_PLACEMENT_3D ( 'NONE', #38675, #72783, #105343 ) ;
#108689=CARTESIAN_POINT ( 'NONE',  ( 13.82816939922343380, -14.24070752338414003, 4.000000000000000000 ) ) ;
#108690=DIRECTION ( 'NONE',  ( -0.000000000000000000, 0.000000000000000000, 1.000000000000000000 ) ) ;
#108691=CARTESIAN_POINT ( 'NONE',  ( 33.79289321881322650, 0.7592924766157104211, 5.000000000000000000 ) ) ;
#108692=VERTEX_POINT ( 'NONE', #17519 ) ;
#108693=ORIENTED_EDGE ( 'NONE', *, *, #112928, .F. ) ;
#108695=ORIENTED_EDGE ( 'NONE', *, *, #138282, .F. ) ;
#108696=VECTOR ( 'NONE', #113221, 1000.000000000000114 ) ;
#108698=VECTOR ( 'NONE', #97229, 1000.000000000000000 ) ;
#108700=CARTESIAN_POINT ( 'NONE',  ( -6.299744871391586898, -27.71228299555210484, 4.000000000000000000 ) ) ;
#108701=LINE ( 'NONE', #118157, #130596 ) ;
#108702=ORIENTED_EDGE ( 'NONE', *, *, #1559, .T. ) ;
#108703=LINE ( 'NONE', #140644, #53015 ) ;
#108704=VECTOR ( 'NONE', #95783, 1000.000000000000000 ) ;
#108705=EDGE_CURVE ( 'NONE', #74278, #96665, #5904, .T. ) ;
#108706=CARTESIAN_POINT ( 'NONE',  ( 8.994519915287490619, 28.92564299267944250, 4.000000000000000000 ) ) ;
#108707=CARTESIAN_POINT ( 'NONE',  ( 13.49999999999990763, 3.653845994658403651, -4.504631822206401459 ) ) ;
#108709=CARTESIAN_POINT ( 'NONE',  ( -24.79289321881328334, 15.75929247661555799, 5.000000000000000000 ) ) ;
#108711=DIRECTION ( 'NONE',  ( 0.7071067811865487940, 0.7071067811865463515, -0.000000000000000000 ) ) ;
#108713=VERTEX_POINT ( 'NONE', #61776 ) ;
#108714=VECTOR ( 'NONE', #72448, 1000.000000000000000 ) ;
#108715=EDGE_CURVE ( 'NONE', #47367, #4770, #37885, .T. ) ;
#108716=DIRECTION ( 'NONE',  ( -0.7071067811865486830, -0.7071067811865464625, 0.000000000000000000 ) ) ;
#108717=VERTEX_POINT ( 'NONE', #61099 ) ;
#108718=ORIENTED_EDGE ( 'NONE', *, *, #119137, .F. ) ;
#108719=VECTOR ( 'NONE', #70969, 1000.000000000000000 ) ;
#108720=ADVANCED_FACE ( 'NONE', ( #105254 ), #59641, .F. ) ;
#108722=VECTOR ( 'NONE', #91677, 1000.000000000000227 ) ;
#108723=CARTESIAN_POINT ( 'NONE',  ( 0.000000000000000000, 0.000000000000000000, 5.000000000000000000 ) ) ;
#108725=CARTESIAN_POINT ( 'NONE',  ( -20.99999999999985079, 13.55218569542903140, 5.000000000000000000 ) ) ;
#108727=DIRECTION ( 'NONE',  ( -0.7071067811865486830, -0.7071067811865464625, -0.000000000000000000 ) ) ;
#108730=LINE ( 'NONE', #85570, #111554 ) ;
#108731=DIRECTION ( 'NONE',  ( -0.000000000000000000, -0.000000000000000000, 1.000000000000000000 ) ) ;
#108732=CARTESIAN_POINT ( 'NONE',  ( 22.42820000000000036, 3.174999999999997158, 1.444000000000000394 ) ) ;
#108733=CARTESIAN_POINT ( 'NONE',  ( 0.1839886062690032631, 28.73617430169787568, 5.000000000000000000 ) ) ;
#108734=VECTOR ( 'NONE', #56581, 1000.000000000000000 ) ;
#108735=DIRECTION ( 'NONE',  ( 0.6830127018922181881, 0.6830127018922202975, -0.2588190451025214056 ) ) ;
#108736=PLANE ( 'NONE',  #83002 ) ;
#108738=FACE_OUTER_BOUND ( 'NONE', #97445, .T. ) ;
#108740=EDGE_CURVE ( 'NONE', #105598, #56006, #114686, .T. ) ;
#108741=VERTEX_POINT ( 'NONE', #127741 ) ;
#108742=EDGE_LOOP ( 'NONE', ( #19598, #22910, #134459, #69877 ) ) ;
#108744=VERTEX_POINT ( 'NONE', #117530 ) ;
#108745=VERTEX_POINT ( 'NONE', #39304 ) ;
#108746=ORIENTED_EDGE ( 'NONE', *, *, #73760, .F. ) ;
#108747=CARTESIAN_POINT ( 'NONE',  ( -0.5166543864104510275, 22.22500000000000142, 4.500000000000000888 ) ) ;
#108749=VECTOR ( 'NONE', #16137, 1000.000000000000227 ) ;
#108750=VERTEX_POINT ( 'NONE', #15355 ) ;
#108751=CARTESIAN_POINT ( 'NONE',  ( 34.92499999999998295, -22.22500000000000142, 4.500000000000000888 ) ) ;
#108754=LINE ( 'NONE', #74767, #55834 ) ;
#108755=VERTEX_POINT ( 'NONE', #103797 ) ;
#108757=CARTESIAN_POINT ( 'NONE',  ( 20.29289321881331887, 14.25929247661557397, 5.000000000000000000 ) ) ;
#108758=CARTESIAN_POINT ( 'NONE',  ( -34.92500000000001137, 16.70193056682083821, 4.500000000000000888 ) ) ;
#108759=FACE_OUTER_BOUND ( 'NONE', #110043, .T. ) ;
#108762=CARTESIAN_POINT ( 'NONE',  ( -14.81601139373099585, 28.73617430169776910, 5.000000000000000000 ) ) ;
#108763=ORIENTED_EDGE ( 'NONE', *, *, #30756, .F. ) ;
#108764=EDGE_LOOP ( 'NONE', ( #31994, #139307, #56941, #79223 ) ) ;
#108765=EDGE_CURVE ( 'NONE', #60766, #42962, #29123, .T. ) ;
#108768=PLANE ( 'NONE',  #92596 ) ;
#108769=EDGE_CURVE ( 'NONE', #51451, #35489, #92952, .T. ) ;
#108772=DIRECTION ( 'NONE',  ( 0.7071067811865487940, 0.7071067811865463515, 0.000000000000000000 ) ) ;
#108773=EDGE_CURVE ( 'NONE', #66690, #95326, #50883, .T. ) ;
#108774=EDGE_CURVE ( 'NONE', #74659, #105294, #126295, .T. ) ;
#108775=CARTESIAN_POINT ( 'NONE',  ( -20.99999999999985789, 13.93112307739204070, 4.000000000000000000 ) ) ;
#108777=AXIS2_PLACEMENT_3D ( 'NONE', #54902, #11335, #99811 ) ;
#108779=ORIENTED_EDGE ( 'NONE', *, *, #130976, .T. ) ;
#108780=VERTEX_POINT ( 'NONE', #26976 ) ;
#108781=PLANE ( 'NONE',  #64682 ) ;
#108782=VECTOR ( 'NONE', #126879, 1000.000000000000227 ) ;
#108785=DIRECTION ( 'NONE',  ( -0.000000000000000000, -0.3543493200069152693, 0.9351131265310292928 ) ) ;
#108787=AXIS2_PLACEMENT_3D ( 'NONE', #94423, #84311, #7404 ) ;
#108788=LINE ( 'NONE', #130606, #127464 ) ;
#108789=EDGE_LOOP ( 'NONE', ( #20368, #42709, #97248, #47453 ) ) ;
#108791=EDGE_CURVE ( 'NONE', #136929, #27557, #47527, .T. ) ;
#108792=ORIENTED_EDGE ( 'NONE', *, *, #25078, .F. ) ;
#108793=CARTESIAN_POINT ( 'NONE',  ( 19.05000000000000071, 3.174999999999997158, 5.000000000000000000 ) ) ;
#108795=DIRECTION ( 'NONE',  ( 0.7071067811865487940, -0.7071067811865463515, 0.000000000000000000 ) ) ;
#108797=DIRECTION ( 'NONE',  ( 0.7071067811865486830, -0.7071067811865464625, -0.000000000000000000 ) ) ;
#108799=EDGE_CURVE ( 'NONE', #40076, #105497, #86379, .T. ) ;
#108801=ORIENTED_EDGE ( 'NONE', *, *, #90459, .T. ) ;
#108802=PLANE ( 'NONE',  #71094 ) ;
#108803=ORIENTED_EDGE ( 'NONE', *, *, #44240, .F. ) ;
#108804=ORIENTED_EDGE ( 'NONE', *, *, #136303, .F. ) ;
#108805=VECTOR ( 'NONE', #62237, 1000.000000000000000 ) ;
#108806=EDGE_CURVE ( 'NONE', #22653, #62049, #97955, .T. ) ;
#108807=ORIENTED_EDGE ( 'NONE', *, *, #126915, .F. ) ;
#108810=DIRECTION ( 'NONE',  ( -0.7071067811865486830, -0.7071067811865464625, -0.000000000000000000 ) ) ;
#108811=CARTESIAN_POINT ( 'NONE',  ( -26.99999999999980815, -9.412538124160660047, 4.000000000000000000 ) ) ;
#108812=ORIENTED_EDGE ( 'NONE', *, *, #19186, .F. ) ;
#108813=CARTESIAN_POINT ( 'NONE',  ( 27.51665438641025219, 22.22500000000000142, 4.500000000000000888 ) ) ;
#108815=EDGE_CURVE ( 'NONE', #88886, #52530, #52995, .T. ) ;
#108816=FACE_OUTER_BOUND ( 'NONE', #112699, .T. ) ;
#108818=DIRECTION ( 'NONE',  ( -0.6830127018922180770, -0.6830127018922204085, -0.2588190451025213501 ) ) ;
#108819=FACE_BOUND ( 'NONE', #137568, .T. ) ;
#108821=CARTESIAN_POINT ( 'NONE',  ( 1.500000000000001332, 19.46639925780206326, 5.000000000000000000 ) ) ;
#108826=FACE_OUTER_BOUND ( 'NONE', #140489, .T. ) ;
#108829=VERTEX_POINT ( 'NONE', #118249 ) ;
#108830=PLANE ( 'NONE',  #88873 ) ;
#108831=ORIENTED_EDGE ( 'NONE', *, *, #74311, .T. ) ;
#108832=EDGE_CURVE ( 'NONE', #50033, #2047, #20359, .T. ) ;
#108834=EDGE_LOOP ( 'NONE', ( #117825, #8985, #66135, #91481 ) ) ;
#108836=LINE ( 'NONE', #120414, #44081 ) ;
#108839=ORIENTED_EDGE ( 'NONE', *, *, #95489, .T. ) ;
#108840=CARTESIAN_POINT ( 'NONE',  ( -16.49999999999988276, 9.052185695429079360, 5.000000000000000000 ) ) ;
#108841=VECTOR ( 'NONE', #107357, 1000.000000000000000 ) ;
#108842=CARTESIAN_POINT ( 'NONE',  ( 10.56687199751251249, -21.74070752338406365, 6.915939825044048028 ) ) ;
#108843=FACE_OUTER_BOUND ( 'NONE', #48792, .T. ) ;
#108847=CARTESIAN_POINT ( 'NONE',  ( 18.48921356237309510, -27.52281430457068367, 5.000000000000000000 ) ) ;
#108848=ORIENTED_EDGE ( 'NONE', *, *, #9560, .F. ) ;
#108849=ORIENTED_EDGE ( 'NONE', *, *, #88071, .F. ) ;
#108851=ORIENTED_EDGE ( 'NONE', *, *, #2686, .F. ) ;
#108853=DIRECTION ( 'NONE',  ( -0.6830127018922181881, 0.6830127018922202975, -0.2588190451025214056 ) ) ;
#108854=VERTEX_POINT ( 'NONE', #42881 ) ;
#108855=ORIENTED_EDGE ( 'NONE', *, *, #128156, .F. ) ;
#108856=PLANE ( 'NONE',  #104490 ) ;
#108857=CARTESIAN_POINT ( 'NONE',  ( 36.18398860626899705, 28.73617430169812437, 5.000000000000000000 ) ) ;
#108858=DIRECTION ( 'NONE',  ( -0.7071067811865486830, -0.7071067811865464625, -0.000000000000000000 ) ) ;
#108859=VERTEX_POINT ( 'NONE', #98652 ) ;
#108860=LINE ( 'NONE', #74876, #122750 ) ;
#108863=DIRECTION ( 'NONE',  ( 0.7071067811865486830, -0.7071067811865464625, -0.000000000000000000 ) ) ;
#108864=ORIENTED_EDGE ( 'NONE', *, *, #72203, .F. ) ;
#108866=LINE ( 'NONE', #111015, #95147 ) ;
#108867=EDGE_CURVE ( 'NONE', #101520, #72881, #88519, .T. ) ;
#108868=DIRECTION ( 'NONE',  ( 0.7071067811865486830, -0.7071067811865464625, -0.000000000000000000 ) ) ;
#108869=PLANE ( 'NONE',  #135153 ) ;
#108870=ORIENTED_EDGE ( 'NONE', *, *, #10702, .T. ) ;
#108871=DIRECTION ( 'NONE',  ( 0.7071067811865487940, -0.7071067811865463515, 0.000000000000000000 ) ) ;
#108872=ORIENTED_EDGE ( 'NONE', *, *, #116922, .T. ) ;
#108873=DIRECTION ( 'NONE',  ( -0.7071067811865486830, -0.7071067811865464625, -0.000000000000000000 ) ) ;
#108874=VECTOR ( 'NONE', #43878, 1000.000000000000000 ) ;
#108875=PLANE ( 'NONE',  #12233 ) ;
#108877=ORIENTED_EDGE ( 'NONE', *, *, #16436, .T. ) ;
#108880=DIRECTION ( 'NONE',  ( -0.7071067811865486830, 0.7071067811865464625, 0.000000000000000000 ) ) ;
#108881=LINE ( 'NONE', #21191, #58340 ) ;
#108882=ORIENTED_EDGE ( 'NONE', *, *, #96901, .T. ) ;
#108883=VECTOR ( 'NONE', #10803, 1000.000000000000000 ) ;
#108886=CARTESIAN_POINT ( 'NONE',  ( -78.48921356237309510, -27.52281430457109934, 5.000000000000000000 ) ) ;
#108888=CARTESIAN_POINT ( 'NONE',  ( -25.49999999999982236, -9.462702396501025959, -9.474982329943454573 ) ) ;
#108889=AXIS2_PLACEMENT_3D ( 'NONE', #54886, #1172, #78064 ) ;
#108890=ORIENTED_EDGE ( 'NONE', *, *, #66140, .T. ) ;
#108891=CARTESIAN_POINT ( 'NONE',  ( -9.489213562373095101, -27.52281430457062328, 5.000000000000000000 ) ) ;
#108892=DIRECTION ( 'NONE',  ( 0.6830127018922181881, 0.6830127018922202975, -0.2588190451025214056 ) ) ;
#108893=EDGE_CURVE ( 'NONE', #57800, #128877, #76944, .T. ) ;
#108894=VERTEX_POINT ( 'NONE', #65356 ) ;
#108895=EDGE_CURVE ( 'NONE', #69740, #107875, #63223, .T. ) ;
#108896=VERTEX_POINT ( 'NONE', #9476 ) ;
#108898=VECTOR ( 'NONE', #86344, 1000.000000000000000 ) ;
#108899=CARTESIAN_POINT ( 'NONE',  ( 36.29974487139159578, -27.71228299555231445, 4.000000000000000000 ) ) ;
#108900=ADVANCED_FACE ( 'NONE', ( #53753 ), #8057, .T. ) ;
#108902=CARTESIAN_POINT ( 'NONE',  ( -8.999999999999932498, -15.03360074219758324, 5.000000000000000000 ) ) ;
#108903=PLANE ( 'NONE',  #132439 ) ;
#108904=EDGE_LOOP ( 'NONE', ( #120708, #32695, #36391, #111791 ) ) ;
#108906=DIRECTION ( 'NONE',  ( -0.6830127018922180770, -0.6830127018922204085, -0.2588190451025213501 ) ) ;
#108907=CARTESIAN_POINT ( 'NONE',  ( -12.00548008471251293, 28.92564299267929684, 4.000000000000000000 ) ) ;
#108908=CARTESIAN_POINT ( 'NONE',  ( -2.700255128608413990, -27.71228299555204089, 4.000000000000000000 ) ) ;
#108909=VECTOR ( 'NONE', #25115, 999.9999999999998863 ) ;
#108910=DIRECTION ( 'NONE',  ( -0.3543493200069162685, -0.000000000000000000, -0.9351131265310288487 ) ) ;
#108913=EDGE_CURVE ( 'NONE', #78506, #125898, #54472, .T. ) ;
#108914=VECTOR ( 'NONE', #79664, 1000.000000000000000 ) ;
#108916=ORIENTED_EDGE ( 'NONE', *, *, #10173, .F. ) ;
#108917=DIRECTION ( 'NONE',  ( -0.7071067811865486830, -0.7071067811865464625, -0.000000000000000000 ) ) ;
#108918=VECTOR ( 'NONE', #27737, 1000.000000000000000 ) ;
#108919=ORIENTED_EDGE ( 'NONE', *, *, #122635, .F. ) ;
#108921=ORIENTED_EDGE ( 'NONE', *, *, #111727, .T. ) ;
#108922=CARTESIAN_POINT ( 'NONE',  ( 9.799968779831573329, 8.259292476615627265, 16.85664084051838785 ) ) ;
#108923=LINE ( 'NONE', #9612, #124887 ) ;
#108924=ADVANCED_FACE ( 'NONE', ( #55168 ), #120368, .F. ) ;
#108925=VECTOR ( 'NONE', #18325, 1000.000000000000000 ) ;
#108926=ORIENTED_EDGE ( 'NONE', *, *, #57435, .F. ) ;
#108927=DIRECTION ( 'NONE',  ( 0.7071067811865486830, -0.7071067811865464625, -0.000000000000000000 ) ) ;
#108929=CARTESIAN_POINT ( 'NONE',  ( 28.49999999999981171, 13.56627193232217898, -10.57019076586062134 ) ) ;
#108931=VECTOR ( 'NONE', #44618, 1000.000000000000000 ) ;
#108932=ORIENTED_EDGE ( 'NONE', *, *, #67699, .T. ) ;
#108933=CARTESIAN_POINT ( 'NONE',  ( -18.29974487139159223, -27.71228299555219010, 4.000000000000000000 ) ) ;
#108935=EDGE_CURVE ( 'NONE', #49877, #111950, #41418, .T. ) ;
#108937=CARTESIAN_POINT ( 'NONE',  ( 14.99451991528749595, 28.92564299267948513, 4.000000000000000000 ) ) ;
#108938=CARTESIAN_POINT ( 'NONE',  ( 19.49999999999986500, -12.66682484999664560, -0.6294897503863490229 ) ) ;
#108939=DIRECTION ( 'NONE',  ( 0.7071067811865487940, 0.7071067811865463515, 0.000000000000000000 ) ) ;
#108940=CARTESIAN_POINT ( 'NONE',  ( -78.18398860626899705, 28.73617430169841924, 5.000000000000000000 ) ) ;
#108942=DIRECTION ( 'NONE',  ( 0.7071067811865487940, 0.7071067811865463515, 0.000000000000000000 ) ) ;
#108944=EDGE_LOOP ( 'NONE', ( #39899, #5376, #142038, #17427 ) ) ;
#108945=ORIENTED_EDGE ( 'NONE', *, *, #128941, .F. ) ;
#108947=LINE ( 'NONE', #2132, #88715 ) ;
#108948=DIRECTION ( 'NONE',  ( -0.000000000000000000, -0.000000000000000000, 1.000000000000000000 ) ) ;
#108949=EDGE_CURVE ( 'NONE', #38542, #79128, #74804, .T. ) ;
#108950=VECTOR ( 'NONE', #92731, 999.9999999999998863 ) ;
#108951=DIRECTION ( 'NONE',  ( -0.7071067811865487940, 0.7071067811865463515, -0.000000000000000000 ) ) ;
#108952=ORIENTED_EDGE ( 'NONE', *, *, #52305, .F. ) ;
#108954=CARTESIAN_POINT ( 'NONE',  ( 28.56687199751240414, -21.74070752338405654, 6.915939825044008060 ) ) ;
#108956=ADVANCED_FACE ( 'NONE', ( #102954 ), #89223, .F. ) ;
#108958=ORIENTED_EDGE ( 'NONE', *, *, #69363, .F. ) ;
#108960=VERTEX_POINT ( 'NONE', #113092 ) ;
#108961=ORIENTED_EDGE ( 'NONE', *, *, #71755, .T. ) ;
#108962=VECTOR ( 'NONE', #60072, 1000.000000000000000 ) ;
#108963=CARTESIAN_POINT ( 'NONE',  ( 54.48921356237310221, -27.52281430457093236, 5.000000000000000000 ) ) ;
#108964=EDGE_CURVE ( 'NONE', #47828, #106324, #45740, .T. ) ;
#108966=DIRECTION ( 'NONE',  ( 0.000000000000000000, 0.000000000000000000, -1.000000000000000000 ) ) ;
#108967=CARTESIAN_POINT ( 'NONE',  ( -11.99451991528749417, 28.92564299267946382, 4.000000000000000000 ) ) ;
#108968=VERTEX_POINT ( 'NONE', #22490 ) ;
#108969=ADVANCED_FACE ( 'NONE', ( #79818 ), #66756, .F. ) ;
#108970=DIRECTION ( 'NONE',  ( -0.000000000000000000, 0.3543493200069153248, 0.9351131265310292928 ) ) ;
#108972=ORIENTED_EDGE ( 'NONE', *, *, #135412, .T. ) ;
#108974=CARTESIAN_POINT ( 'NONE',  ( 20.14818355038132580, 17.25929247661554200, 8.802941693769250620 ) ) ;
#108975=CARTESIAN_POINT ( 'NONE',  ( 26.99999999999980815, 20.70535890316563155, 1.956823837851852987 ) ) ;
#108976=FACE_OUTER_BOUND ( 'NONE', #123873, .T. ) ;
#108977=AXIS2_PLACEMENT_3D ( 'NONE', #125001, #25681, #136577 ) ;
#108978=VECTOR ( 'NONE', #142110, 999.9999999999998863 ) ;
#108980=EDGE_CURVE ( 'NONE', #129678, #7365, #134156, .T. ) ;
#108981=DIRECTION ( 'NONE',  ( 1.000000000000000000, 0.000000000000000000, 0.000000000000000000 ) ) ;
#108983=PLANE ( 'NONE',  #136735 ) ;
#108984=LINE ( 'NONE', #74988, #15365 ) ;
#108986=VERTEX_POINT ( 'NONE', #47200 ) ;
#108987=ORIENTED_EDGE ( 'NONE', *, *, #141166, .T. ) ;
#108988=PLANE ( 'NONE',  #97790 ) ;
#108990=VECTOR ( 'NONE', #138551, 1000.000000000000000 ) ;
#108991=EDGE_CURVE ( 'NONE', #80231, #47388, #7655, .T. ) ;
#108992=ORIENTED_EDGE ( 'NONE', *, *, #15796, .T. ) ;
#108994=VECTOR ( 'NONE', #126652, 1000.000000000000000 ) ;
#108995=ORIENTED_EDGE ( 'NONE', *, *, #28023, .F. ) ;
#108996=CARTESIAN_POINT ( 'NONE',  ( 3.516654386410431599, 22.22500000000000142, 4.500000000000000888 ) ) ;
#108997=EDGE_LOOP ( 'NONE', ( #99497, #121525, #10971, #38727 ) ) ;
#108998=DIRECTION ( 'NONE',  ( -0.7071067811865487940, 0.7071067811865463515, -0.000000000000000000 ) ) ;
#108999=CARTESIAN_POINT ( 'NONE',  ( -9.489213562373095101, -27.52281430457062328, 5.000000000000000000 ) ) ;
#109000=AXIS2_PLACEMENT_3D ( 'NONE', #110315, #132843, #11711 ) ;
#109004=LINE ( 'NONE', #9698, #14033 ) ;
#109005=FACE_BOUND ( 'NONE', #98199, .T. ) ;
#109006=CARTESIAN_POINT ( 'NONE',  ( -36.87485380690743852, -14.24070752338414003, 9.401115078912742007 ) ) ;
#109007=DIRECTION ( 'NONE',  ( -0.6830127018922181881, 0.6830127018922202975, -0.2588190451025214056 ) ) ;
#109008=EDGE_CURVE ( 'NONE', #118949, #59656, #123297, .T. ) ;
#109009=AXIS2_PLACEMENT_3D ( 'NONE', #131643, #18549, #87425 ) ;
#109010=CARTESIAN_POINT ( 'NONE',  ( -20.99451991528748707, 28.92564299267952777, 4.000000000000000000 ) ) ;
#109015=ORIENTED_EDGE ( 'NONE', *, *, #137147, .T. ) ;
#109016=EDGE_CURVE ( 'NONE', #143327, #10069, #55898, .T. ) ;
#109019=EDGE_LOOP ( 'NONE', ( #46961, #79458, #132752, #18310 ) ) ;
#109020=LINE ( 'NONE', #129352, #87016 ) ;
#109021=AXIS2_PLACEMENT_3D ( 'NONE', #19687, #107414, #40749 ) ;
#109022=LINE ( 'NONE', #66976, #28119 ) ;
#109023=VECTOR ( 'NONE', #61388, 999.9999999999998863 ) ;
#109027=LINE ( 'NONE', #140947, #79635 ) ;
#109028=FACE_OUTER_BOUND ( 'NONE', #130161, .T. ) ;
#109029=VECTOR ( 'NONE', #22660, 1000.000000000000000 ) ;
#109030=CARTESIAN_POINT ( 'NONE',  ( -34.92500000000001137, -10.29806943317888290, 4.500000000000000888 ) ) ;
#109031=LINE ( 'NONE', #30045, #66698 ) ;
#109032=VECTOR ( 'NONE', #15071, 1000.000000000000000 ) ;
#109034=CARTESIAN_POINT ( 'NONE',  ( 17.90156419391752962, 11.25929247661561305, 10.79108189686411023 ) ) ;
#109035=ORIENTED_EDGE ( 'NONE', *, *, #59136, .T. ) ;
#109036=LINE ( 'NONE', #143111, #114013 ) ;
#109037=ORIENTED_EDGE ( 'NONE', *, *, #107376, .F. ) ;
#109039=CARTESIAN_POINT ( 'NONE',  ( 20.67183060077632817, 17.25929247661554200, 4.000000000000000000 ) ) ;
#109042=EDGE_LOOP ( 'NONE', ( #4326, #98751, #62505 ) ) ;
#109044=ORIENTED_EDGE ( 'NONE', *, *, #9348, .T. ) ;
#109046=ORIENTED_EDGE ( 'NONE', *, *, #98632, .T. ) ;
#109047=LINE ( 'NONE', #98200, #85685 ) ;
#109048=CARTESIAN_POINT ( 'NONE',  ( 20.99999999999985434, -7.447814304570756327, 5.000000000000000000 ) ) ;
#109052=ORIENTED_EDGE ( 'NONE', *, *, #101946, .F. ) ;
#109053=CARTESIAN_POINT ( 'NONE',  ( -33.18398860626899705, 28.73617430169810305, 5.000000000000000000 ) ) ;
#109054=ORIENTED_EDGE ( 'NONE', *, *, #28998, .F. ) ;
#109055=DIRECTION ( 'NONE',  ( -0.3543493200069162685, -0.000000000000000000, -0.9351131265310288487 ) ) ;
#109056=VECTOR ( 'NONE', #45541, 1000.000000000000000 ) ;
#109057=DIRECTION ( 'NONE',  ( -0.7071067811865487940, 0.7071067811865463515, 0.000000000000000000 ) ) ;
#109058=DIRECTION ( 'NONE',  ( -0.000000000000000000, -0.3543493200069152693, 0.9351131265310292928 ) ) ;
#109059=ORIENTED_EDGE ( 'NONE', *, *, #41405, .T. ) ;
#109060=AXIS2_PLACEMENT_3D ( 'NONE', #123029, #57081, #9964 ) ;
#109061=ORIENTED_EDGE ( 'NONE', *, *, #28340, .F. ) ;
#109062=CARTESIAN_POINT ( 'NONE',  ( -1.499999999999987566, 7.466399257802191158, 5.000000000000000000 ) ) ;
#109063=DIRECTION ( 'NONE',  ( -0.7071067811865486830, 0.7071067811865464625, 0.000000000000000000 ) ) ;
#109064=CARTESIAN_POINT ( 'NONE',  ( 31.49999999999977973, 0.4311230773921780335, 4.000000000000000000 ) ) ;
#109065=ORIENTED_EDGE ( 'NONE', *, *, #14587, .F. ) ;
#109066=DIRECTION ( 'NONE',  ( 0.6830127018922180770, -0.6830127018922204085, -0.2588190451025213501 ) ) ;
#109067=ORIENTED_EDGE ( 'NONE', *, *, #92785, .F. ) ;
#109068=ORIENTED_EDGE ( 'NONE', *, *, #134251, .T. ) ;
#109069=ORIENTED_EDGE ( 'NONE', *, *, #135330, .T. ) ;
#109070=VECTOR ( 'NONE', #86794, 1000.000000000000000 ) ;
#109071=FACE_OUTER_BOUND ( 'NONE', #64252, .T. ) ;
#109073=AXIS2_PLACEMENT_3D ( 'NONE', #88446, #133376, #143513 ) ;
#109074=DIRECTION ( 'NONE',  ( 1.000000000000000000, 0.000000000000000000, 0.000000000000000000 ) ) ;
#109076=DIRECTION ( 'NONE',  ( -0.6830127018922180770, -0.6830127018922204085, -0.2588190451025213501 ) ) ;
#109077=ADVANCED_FACE ( 'NONE', ( #45044 ), #133445, .T. ) ;
#109078=CARTESIAN_POINT ( 'NONE',  ( -12.75860074219786711, 21.72500000000000142, 5.000000000000000000 ) ) ;
#109079=CARTESIAN_POINT ( 'NONE',  ( 27.48921356237309155, -27.52281430457074762, 5.000000000000000000 ) ) ;
#109080=EDGE_CURVE ( 'NONE', #2427, #126541, #46471, .T. ) ;
#109081=EDGE_CURVE ( 'NONE', #97758, #141006, #35591, .T. ) ;
#109082=ORIENTED_EDGE ( 'NONE', *, *, #91339, .T. ) ;
#109083=DIRECTION ( 'NONE',  ( 0.7071067811865487940, 0.7071067811865463515, 0.000000000000000000 ) ) ;
#109084=VERTEX_POINT ( 'NONE', #23213 ) ;
#109087=ADVANCED_FACE ( 'NONE', ( #24660 ), #80498, .F. ) ;
#109088=ADVANCED_FACE ( 'NONE', ( #12353 ), #94189, .T. ) ;
#109090=VERTEX_POINT ( 'NONE', #127552 ) ;
#109092=DIRECTION ( 'NONE',  ( 1.000000000000000000, 0.000000000000000000, 0.000000000000000000 ) ) ;
#109093=ORIENTED_EDGE ( 'NONE', *, *, #106018, .T. ) ;
#109095=EDGE_CURVE ( 'NONE', #41713, #134257, #4268, .T. ) ;
#109096=LINE ( 'NONE', #43158, #53387 ) ;
#109097=DIRECTION ( 'NONE',  ( 0.7071067811865486830, -0.7071067811865464625, -0.000000000000000000 ) ) ;
#109098=FACE_OUTER_BOUND ( 'NONE', #83794, .T. ) ;
#109100=VECTOR ( 'NONE', #20275, 999.9999999999998863 ) ;
#109101=LINE ( 'NONE', #33023, #43584 ) ;
#109103=CARTESIAN_POINT ( 'NONE',  ( 22.42820000000000036, 3.174999999999997158, 1.444000000000000394 ) ) ;
#109104=VECTOR ( 'NONE', #16128, 1000.000000000000227 ) ;
#109105=ADVANCED_FACE ( 'NONE', ( #137733 ), #139163, .T. ) ;
#109106=VECTOR ( 'NONE', #44529, 1000.000000000000000 ) ;
#109107=CARTESIAN_POINT ( 'NONE',  ( -14.20710678118643244, -14.24070752338413648, 5.000000000000000000 ) ) ;
#109108=CARTESIAN_POINT ( 'NONE',  ( 1.637538124160967001, 22.22500000000000142, 4.000000000000000000 ) ) ;
#109109=CARTESIAN_POINT ( 'NONE',  ( 33.29974487139158867, -27.71228299555229313, 4.000000000000000000 ) ) ;
#109110=VERTEX_POINT ( 'NONE', #136276 ) ;
#109111=CARTESIAN_POINT ( 'NONE',  ( -10.49999999999992184, 21.43112307739196609, 4.000000000000000000 ) ) ;
#109113=VECTOR ( 'NONE', #31200, 1000.000000000000227 ) ;
#109115=VECTOR ( 'NONE', #63687, 1000.000000000000227 ) ;
#109116=DIRECTION ( 'NONE',  ( -0.6830127018922180770, -0.6830127018922204085, -0.2588190451025213501 ) ) ;
#109117=AXIS2_PLACEMENT_3D ( 'NONE', #1969, #69445, #125234 ) ;
#109118=PLANE ( 'NONE',  #119382 ) ;
#109120=VECTOR ( 'NONE', #106739, 1000.000000000000227 ) ;
#109121=DIRECTION ( 'NONE',  ( 0.3543493200069162685, -0.000000000000000000, -0.9351131265310288487 ) ) ;
#109122=DIRECTION ( 'NONE',  ( -0.6830127018922181881, 0.6830127018922202975, -0.2588190451025214056 ) ) ;
#109124=CARTESIAN_POINT ( 'NONE',  ( -18.48921356237309510, -27.52281430457068367, 5.000000000000000000 ) ) ;
#109125=LINE ( 'NONE', #54080, #141275 ) ;
#109126=DIRECTION ( 'NONE',  ( -0.6830127018922180770, -0.6830127018922204085, -0.2588190451025213501 ) ) ;
#109128=VERTEX_POINT ( 'NONE', #92766 ) ;
#109129=CARTESIAN_POINT ( 'NONE',  ( -48.48921356237309510, -27.52281430457089328, 5.000000000000000000 ) ) ;
#109130=CARTESIAN_POINT ( 'NONE',  ( 34.42499999999998295, 22.22500000000000142, 5.000000000000000000 ) ) ;
#109131=AXIS2_PLACEMENT_3D ( 'NONE', #117686, #8215, #64067 ) ;
#109132=EDGE_CURVE ( 'NONE', #43296, #16866, #5739, .T. ) ;
#109133=LINE ( 'NONE', #19278, #100554 ) ;
#109134=CARTESIAN_POINT ( 'NONE',  ( -0.7175773864256695944, -21.73023691814493219, 5.000000000000000888 ) ) ;
#109136=CARTESIAN_POINT ( 'NONE',  ( -20.33153258840131272, -18.74070752338409207, 20.73178291233836390 ) ) ;
#109137=CARTESIAN_POINT ( 'NONE',  ( 23.67183060077630330, -9.740707523384186217, 4.000000000000000000 ) ) ;
#109138=VERTEX_POINT ( 'NONE', #60916 ) ;
#109140=VECTOR ( 'NONE', #43090, 1000.000000000000000 ) ;
#109141=CARTESIAN_POINT ( 'NONE',  ( -54.48921356237310221, -27.52281430457093236, 5.000000000000000000 ) ) ;
#109144=EDGE_CURVE ( 'NONE', #27298, #134862, #136375, .T. ) ;
#109145=VERTEX_POINT ( 'NONE', #36963 ) ;
#109146=AXIS2_PLACEMENT_3D ( 'NONE', #68250, #80526, #59493 ) ;
#109147=CARTESIAN_POINT ( 'NONE',  ( -0.4892135623730947680, -27.52281430457055578, 5.000000000000000000 ) ) ;
#109148=EDGE_CURVE ( 'NONE', #58827, #50577, #81217, .T. ) ;
#109152=EDGE_CURVE ( 'NONE', #55852, #45578, #83341, .T. ) ;
#109153=VECTOR ( 'NONE', #143291, 1000.000000000000000 ) ;
#109154=DIRECTION ( 'NONE',  ( -0.7071067811865486830, -0.7071067811865464625, 0.000000000000000000 ) ) ;
#109155=CARTESIAN_POINT ( 'NONE',  ( -4.828169399223493308, 15.75929247661555799, 4.000000000000000000 ) ) ;
#109157=AXIS2_PLACEMENT_3D ( 'NONE', #129628, #30329, #94845 ) ;
#109158=LINE ( 'NONE', #9841, #60476 ) ;
#109159=ADVANCED_FACE ( 'NONE', ( #17353 ), #125423, .F. ) ;
#109160=LINE ( 'NONE', #43212, #88240 ) ;
#109161=CARTESIAN_POINT ( 'NONE',  ( 25.49999999999982592, -17.91344420646039737, 1.358650452708521916 ) ) ;
#109162=CARTESIAN_POINT ( 'NONE',  ( 31.49999999999978684, 21.43112307739196964, 4.000000000000000000 ) ) ;
#109163=CARTESIAN_POINT ( 'NONE',  ( 34.49999999999975842, -8.945670655168960650, 4.994342998332163219 ) ) ;
#109166=DIRECTION ( 'NONE',  ( -0.000000000000000000, 0.000000000000000000, 1.000000000000000000 ) ) ;
#109167=LINE ( 'NONE', #77296, #820 ) ;
#109168=ADVANCED_FACE ( 'NONE', ( #93497 ), #105764, .F. ) ;
#109169=DIRECTION ( 'NONE',  ( -0.6830127018922181881, 0.6830127018922202975, -0.2588190451025214056 ) ) ;
#109170=ORIENTED_EDGE ( 'NONE', *, *, #115532, .F. ) ;
#109173=EDGE_LOOP ( 'NONE', ( #99562, #68918, #75476, #4689 ) ) ;
#109174=ADVANCED_FACE ( 'NONE', ( #70366 ), #126816, .F. ) ;
#109175=DIRECTION ( 'NONE',  ( 0.7071067811865486830, -0.7071067811865464625, -0.000000000000000000 ) ) ;
#109176=CARTESIAN_POINT ( 'NONE',  ( 1.828169399223519731, -8.240707523384200428, 4.000000000000000000 ) ) ;
#109177=VECTOR ( 'NONE', #89217, 1000.000000000000000 ) ;
#109178=CARTESIAN_POINT ( 'NONE',  ( 20.66652290003515446, 8.920938975803856863, 4.000000000000000000 ) ) ;
#109180=ORIENTED_EDGE ( 'NONE', *, *, #7771, .F. ) ;
#109181=AXIS2_PLACEMENT_3D ( 'NONE', #118184, #30508, #97899 ) ;
#109182=DIRECTION ( 'NONE',  ( -0.3543493200069162685, -0.000000000000000000, -0.9351131265310288487 ) ) ;
#109183=ORIENTED_EDGE ( 'NONE', *, *, #72407, .F. ) ;
#109184=EDGE_CURVE ( 'NONE', #135984, #123357, #87280, .T. ) ;
#109185=DIRECTION ( 'NONE',  ( -0.6830127018922180770, -0.6830127018922204085, -0.2588190451025213501 ) ) ;
#109186=DIRECTION ( 'NONE',  ( 1.000000000000000000, 0.000000000000000000, 0.000000000000000000 ) ) ;
#109187=DIRECTION ( 'NONE',  ( 0.7071067811865487940, 0.7071067811865463515, -0.000000000000000000 ) ) ;
#109189=ORIENTED_EDGE ( 'NONE', *, *, #33840, .F. ) ;
#109190=ORIENTED_EDGE ( 'NONE', *, *, #128815, .T. ) ;
#109191=FACE_BOUND ( 'NONE', #71056, .T. ) ;
#109192=CARTESIAN_POINT ( 'NONE',  ( -22.17183060077631396, -17.24070752338410273, 4.000000000000000000 ) ) ;
#109193=EDGE_CURVE ( 'NONE', #54275, #1086, #48566, .T. ) ;
#109194=CARTESIAN_POINT ( 'NONE',  ( -21.48921356237309155, -27.52281430457070499, 5.000000000000000000 ) ) ;
#109198=LINE ( 'NONE', #42554, #139210 ) ;
#109200=ORIENTED_EDGE ( 'NONE', *, *, #37267, .T. ) ;
#109201=EDGE_CURVE ( 'NONE', #138495, #43532, #59231, .T. ) ;
#109202=EDGE_LOOP ( 'NONE', ( #114707, #64016, #124450, #9153 ) ) ;
#109204=ORIENTED_EDGE ( 'NONE', *, *, #67317, .T. ) ;
#109205=ORIENTED_EDGE ( 'NONE', *, *, #96074, .T. ) ;
#109207=AXIS2_PLACEMENT_3D ( 'NONE', #73630, #30857, #119944 ) ;
#109208=VECTOR ( 'NONE', #110296, 1000.000000000000227 ) ;
#109209=CARTESIAN_POINT ( 'NONE',  ( -15.48921356237309510, -27.52281430457066236, 5.000000000000000000 ) ) ;
#109210=VECTOR ( 'NONE', #20427, 999.9999999999998863 ) ;
#109212=DIRECTION ( 'NONE',  ( -0.7071067811865486830, 0.7071067811865464625, 0.000000000000000000 ) ) ;
#109213=EDGE_CURVE ( 'NONE', #17061, #49517, #25109, .T. ) ;
#109214=ORIENTED_EDGE ( 'NONE', *, *, #96680, .T. ) ;
#109215=PLANE ( 'NONE',  #80697 ) ;
#109216=CARTESIAN_POINT ( 'NONE',  ( 21.48921356237309155, -27.52281430457070499, 5.000000000000000000 ) ) ;
#109217=CARTESIAN_POINT ( 'NONE',  ( -21.18398860626899349, 28.73617430169802134, 5.000000000000000000 ) ) ;
#109218=CARTESIAN_POINT ( 'NONE',  ( 27.43680103220812327, -12.74070752338415602, 9.898150129686310805 ) ) ;
#109219=CARTESIAN_POINT ( 'NONE',  ( -15.18398860626900237, 28.73617430169797871, 5.000000000000000000 ) ) ;
#109221=VECTOR ( 'NONE', #64937, 1000.000000000000227 ) ;
#109224=ORIENTED_EDGE ( 'NONE', *, *, #39123, .T. ) ;
#109225=DIRECTION ( 'NONE',  ( -0.7071067811865487940, 0.7071067811865463515, -0.000000000000000000 ) ) ;
#109227=VERTEX_POINT ( 'NONE', #47643 ) ;
#109228=VERTEX_POINT ( 'NONE', #124439 ) ;
#109230=ORIENTED_EDGE ( 'NONE', *, *, #93264, .T. ) ;
#109231=VECTOR ( 'NONE', #7347, 1000.000000000000227 ) ;
#109234=DIRECTION ( 'NONE',  ( -0.6830127018922180770, -0.6830127018922204085, -0.2588190451025213501 ) ) ;
#109237=CARTESIAN_POINT ( 'NONE',  ( 9.096670641874002428, -2.240707523384257716, 15.26439735382754570 ) ) ;
#109238=DIRECTION ( 'NONE',  ( 0.7071067811865486830, -0.7071067811865464625, -0.000000000000000000 ) ) ;
#109239=CARTESIAN_POINT ( 'NONE',  ( 39.18398860626899705, 28.73617430169814568, 5.000000000000000000 ) ) ;
#109240=VERTEX_POINT ( 'NONE', #101257 ) ;
#109241=CARTESIAN_POINT ( 'NONE',  ( 5.207106781186512379, 0.7592924766157120864, 5.000000000000000000 ) ) ;
#109242=LINE ( 'NONE', #9926, #86495 ) ;
#109243=LINE ( 'NONE', #130312, #118520 ) ;
#109245=LINE ( 'NONE', #10627, #140122 ) ;
#109246=ORIENTED_EDGE ( 'NONE', *, *, #73001, .F. ) ;
#109247=VECTOR ( 'NONE', #80162, 1000.000000000000114 ) ;
#109248=CARTESIAN_POINT ( 'NONE',  ( 3.489213562373097322, -27.52281430457057709, 5.000000000000000000 ) ) ;
#109249=ORIENTED_EDGE ( 'NONE', *, *, #137253, .F. ) ;
#109250=VECTOR ( 'NONE', #99990, 1000.000000000000000 ) ;
#109251=ORIENTED_EDGE ( 'NONE', *, *, #110960, .T. ) ;
#109252=VERTEX_POINT ( 'NONE', #91803 ) ;
#109254=ORIENTED_EDGE ( 'NONE', *, *, #18606, .T. ) ;
#109255=VECTOR ( 'NONE', #112883, 1000.000000000000000 ) ;
#109256=CARTESIAN_POINT ( 'NONE',  ( 28.49999999999980460, -19.53360074219753884, 5.000000000000000000 ) ) ;
#109257=DIRECTION ( 'NONE',  ( -0.7071067811865487940, -0.7071067811865463515, -0.000000000000000000 ) ) ;
#109258=ADVANCED_FACE ( 'NONE', ( #91128 ), #123754, .T. ) ;
#109259=EDGE_LOOP ( 'NONE', ( #74236, #106810, #114064, #137040 ) ) ;
#109260=CARTESIAN_POINT ( 'NONE',  ( 17.67183060077634593, -6.740707523384211086, 4.000000000000000000 ) ) ;
#109261=ORIENTED_EDGE ( 'NONE', *, *, #83682, .T. ) ;
#109262=VECTOR ( 'NONE', #54683, 1000.000000000000000 ) ;
#109263=EDGE_CURVE ( 'NONE', #3502, #94791, #46208, .T. ) ;
#109264=EDGE_CURVE ( 'NONE', #55786, #97574, #136026, .T. ) ;
#109267=LINE ( 'NONE', #121560, #60198 ) ;
#109268=EDGE_CURVE ( 'NONE', #46985, #132831, #67970, .T. ) ;
#109269=DIRECTION ( 'NONE',  ( 0.6830127018922180770, -0.6830127018922204085, -0.2588190451025213501 ) ) ;
#109270=DIRECTION ( 'NONE',  ( -0.000000000000000000, 0.3543493200069153248, 0.9351131265310292928 ) ) ;
#109271=ORIENTED_EDGE ( 'NONE', *, *, #141882, .T. ) ;
#109272=VERTEX_POINT ( 'NONE', #14950 ) ;
#109275=ORIENTED_EDGE ( 'NONE', *, *, #133245, .F. ) ;
#109276=CARTESIAN_POINT ( 'NONE',  ( 30.18398860626900060, 28.73617430169808173, 5.000000000000000000 ) ) ;
#109277=VECTOR ( 'NONE', #118750, 1000.000000000000227 ) ;
#109278=ADVANCED_FACE ( 'NONE', ( #79784 ), #123262, .F. ) ;
#109280=LINE ( 'NONE', #12096, #25091 ) ;
#109281=PLANE ( 'NONE',  #54988 ) ;
#109282=EDGE_CURVE ( 'NONE', #63170, #120276, #36239, .T. ) ;
#109283=DIRECTION ( 'NONE',  ( -0.7071067811865486830, 0.7071067811865464625, 0.000000000000000000 ) ) ;
#109285=DIRECTION ( 'NONE',  ( -0.7071067811865486830, -0.7071067811865464625, -0.000000000000000000 ) ) ;
#109286=ORIENTED_EDGE ( 'NONE', *, *, #94469, .T. ) ;
#109287=DIRECTION ( 'NONE',  ( 0.6830127018922180770, -0.6830127018922204085, -0.2588190451025213501 ) ) ;
#109288=ORIENTED_EDGE ( 'NONE', *, *, #72917, .F. ) ;
#109289=LINE ( 'NONE', #63676, #33762 ) ;
#109290=VERTEX_POINT ( 'NONE', #92022 ) ;
#109293=DIRECTION ( 'NONE',  ( -0.7071067811865487940, 0.7071067811865463515, -0.000000000000000000 ) ) ;
#109294=DIRECTION ( 'NONE',  ( -0.7071067811865486830, -0.7071067811865464625, 0.000000000000000000 ) ) ;
#109295=ORIENTED_EDGE ( 'NONE', *, *, #9778, .F. ) ;
#109296=LINE ( 'NONE', #7825, #81608 ) ;
#109297=EDGE_LOOP ( 'NONE', ( #76668, #46639, #120904, #103989 ) ) ;
#109298=CARTESIAN_POINT ( 'NONE',  ( 2.700255128608413990, -27.71228299555204089, 4.000000000000000000 ) ) ;
#109299=VECTOR ( 'NONE', #529, 1000.000000000000000 ) ;
#109300=VERTEX_POINT ( 'NONE', #67459 ) ;
#109301=DIRECTION ( 'NONE',  ( 0.7071067811865487940, -0.7071067811865463515, 0.000000000000000000 ) ) ;
#109302=ORIENTED_EDGE ( 'NONE', *, *, #38960, .F. ) ;
#109303=ADVANCED_FACE ( 'NONE', ( #59439 ), #111652, .F. ) ;
#109304=LINE ( 'NONE', #95565, #133173 ) ;
#109306=LINE ( 'NONE', #53509, #60112 ) ;
#109307=LINE ( 'NONE', #44066, #53169 ) ;
#109308=CARTESIAN_POINT ( 'NONE',  ( -13.49999999999990763, 16.08746187583908238, 4.000000000000000000 ) ) ;
#109309=DIRECTION ( 'NONE',  ( -0.7071067811865486830, -0.7071067811865464625, 0.000000000000000000 ) ) ;
#109313=AXIS2_PLACEMENT_3D ( 'NONE', #84366, #40153, #96589 ) ;
#109317=CARTESIAN_POINT ( 'NONE',  ( 32.99999999999976552, 12.83542986846999945, -1.025386466790447093 ) ) ;
#109318=ORIENTED_EDGE ( 'NONE', *, *, #56835, .F. ) ;
#109319=VERTEX_POINT ( 'NONE', #89876 ) ;
#109320=AXIS2_PLACEMENT_3D ( 'NONE', #131555, #19216, #75059 ) ;
#109321=AXIS2_PLACEMENT_3D ( 'NONE', #30420, #97806, #76065 ) ;
#109322=CARTESIAN_POINT ( 'NONE',  ( -47.99451991528749062, 28.92564299267971251, 4.000000000000000000 ) ) ;
#109324=ADVANCED_FACE ( 'NONE', ( #79058 ), #23934, .T. ) ;
#109325=CARTESIAN_POINT ( 'NONE',  ( -25.49999999999981526, 16.46639925780209879, 5.000000000000000000 ) ) ;
#109326=DIRECTION ( 'NONE',  ( -0.000000000000000000, 0.3543493200069153248, 0.9351131265310292928 ) ) ;
#109328=VECTOR ( 'NONE', #103936, 1000.000000000000227 ) ;
#109329=CARTESIAN_POINT ( 'NONE',  ( 34.45011844616453800, 21.00230414159372216, 5.000000000000001776 ) ) ;
#109330=ORIENTED_EDGE ( 'NONE', *, *, #33086, .F. ) ;
#109332=DIRECTION ( 'NONE',  ( 0.000000000000000000, 1.000000000000000000, 0.000000000000000000 ) ) ;
#109333=ADVANCED_FACE ( 'NONE', ( #2120 ), #104306, .F. ) ;
#109334=LINE ( 'NONE', #10015, #120590 ) ;
#109338=VERTEX_POINT ( 'NONE', #71726 ) ;
#109339=DIRECTION ( 'NONE',  ( 0.7071067811865487940, 0.7071067811865463515, -0.000000000000000000 ) ) ;
#109340=DIRECTION ( 'NONE',  ( -0.000000000000000000, 0.000000000000000000, 1.000000000000000000 ) ) ;
#109342=LINE ( 'NONE', #63720, #128917 ) ;
#109343=EDGE_CURVE ( 'NONE', #123719, #110682, #105042, .T. ) ;
#109344=DIRECTION ( 'NONE',  ( 0.3543493200069162685, -0.000000000000000000, -0.9351131265310288487 ) ) ;
#109346=VERTEX_POINT ( 'NONE', #63004 ) ;
#109347=ORIENTED_EDGE ( 'NONE', *, *, #101502, .T. ) ;
#109350=EDGE_CURVE ( 'NONE', #82894, #43938, #138391, .T. ) ;
#109351=CARTESIAN_POINT ( 'NONE',  ( 21.51665438641029482, 22.22500000000000142, 4.500000000000000888 ) ) ;
#109352=DIRECTION ( 'NONE',  ( 0.6830127018922180770, 0.6830127018922202975, -0.2588190451025213501 ) ) ;
#109353=ORIENTED_EDGE ( 'NONE', *, *, #82956, .T. ) ;
#109355=DIRECTION ( 'NONE',  ( 0.7071067811865487940, 0.7071067811865463515, -0.000000000000000000 ) ) ;
#109356=AXIS2_PLACEMENT_3D ( 'NONE', #17731, #62009, #65598 ) ;
#109358=ORIENTED_EDGE ( 'NONE', *, *, #138454, .T. ) ;
#109359=AXIS2_PLACEMENT_3D ( 'NONE', #9937, #57058, #43302 ) ;
#109360=DIRECTION ( 'NONE',  ( -0.6830127018922180770, -0.6830127018922204085, -0.2588190451025213501 ) ) ;
#109361=ORIENTED_EDGE ( 'NONE', *, *, #64232, .F. ) ;
#109362=EDGE_LOOP ( 'NONE', ( #21438, #101445, #82790, #116280 ) ) ;
#109363=ADVANCED_FACE ( 'NONE', ( #71019 ), #29608, .F. ) ;
#109364=ORIENTED_EDGE ( 'NONE', *, *, #27124, .T. ) ;
#109365=CARTESIAN_POINT ( 'NONE',  ( -27.48921356237309155, -27.52281430457074762, 5.000000000000000000 ) ) ;
#109366=EDGE_CURVE ( 'NONE', #133408, #39160, #7116, .T. ) ;
#109367=DIRECTION ( 'NONE',  ( 0.6830127018922180770, -0.6830127018922204085, -0.2588190451025213501 ) ) ;
#109369=CARTESIAN_POINT ( 'NONE',  ( -8.999999999999928946, 19.55218569542897100, 5.000000000000000000 ) ) ;
#109371=LINE ( 'NONE', #593, #39530 ) ;
#109372=( NAMED_UNIT ( * ) PLANE_ANGLE_UNIT ( ) SI_UNIT ( $, .RADIAN. ) );
#109373=EDGE_CURVE ( 'NONE', #56845, #7390, #93463, .T. ) ;
#109374=VERTEX_POINT ( 'NONE', #115889 ) ;
#109375=VERTEX_POINT ( 'NONE', #84723 ) ;
#109376=FACE_OUTER_BOUND ( 'NONE', #79317, .T. ) ;
#109377=ORIENTED_EDGE ( 'NONE', *, *, #128585, .F. ) ;
#109378=ORIENTED_EDGE ( 'NONE', *, *, #140564, .T. ) ;
#109379=VECTOR ( 'NONE', #50528, 1000.000000000000000 ) ;
#109381=ADVANCED_FACE ( 'NONE', ( #50661 ), #105728, .F. ) ;
#109382=EDGE_CURVE ( 'NONE', #141003, #134564, #126780, .T. ) ;
#109383=CARTESIAN_POINT ( 'NONE',  ( -8.994519915287490619, 28.92564299267944250, 4.000000000000000000 ) ) ;
#109384=ADVANCED_FACE ( 'NONE', ( #39827 ), #95590, .F. ) ;
#109385=ORIENTED_EDGE ( 'NONE', *, *, #86243, .F. ) ;
#109386=CARTESIAN_POINT ( 'NONE',  ( 24.32816939922336630, 14.25929247661557397, 4.000000000000000000 ) ) ;
#109387=CARTESIAN_POINT ( 'NONE',  ( 25.82816939922335209, -5.240707523384228850, 4.000000000000000000 ) ) ;
#109388=CARTESIAN_POINT ( 'NONE',  ( -39.48921356237310221, -27.52281430457082934, 5.000000000000000000 ) ) ;
#109389=PLANE ( 'NONE',  #134087 ) ;
#109391=CARTESIAN_POINT ( 'NONE',  ( -80.99451991528748351, 28.92564299267994699, 4.000000000000000000 ) ) ;
#109392=ORIENTED_EDGE ( 'NONE', *, *, #57956, .T. ) ;
#109393=CARTESIAN_POINT ( 'NONE',  ( 28.49999999999981881, -17.94781430457063820, 5.000000000000000000 ) ) ;
#109394=EDGE_LOOP ( 'NONE', ( #56903, #78678, #24872, #82641 ) ) ;
#109395=CARTESIAN_POINT ( 'NONE',  ( -30.79289321881324781, 9.759292476615621936, 5.000000000000000000 ) ) ;
#109396=ORIENTED_EDGE ( 'NONE', *, *, #124735, .T. ) ;
#109398=ADVANCED_FACE ( 'NONE', ( #15841 ), #51397, .T. ) ;
#109399=VERTEX_POINT ( 'NONE', #72469 ) ;
#109400=CARTESIAN_POINT ( 'NONE',  ( 0.6048623318752055500, 21.75929247661549226, 21.32995629748186417 ) ) ;
#109401=ORIENTED_EDGE ( 'NONE', *, *, #7862, .F. ) ;
#109402=ORIENTED_EDGE ( 'NONE', *, *, #64450, .T. ) ;
#109403=VECTOR ( 'NONE', #26085, 1000.000000000000000 ) ;
#109405=CARTESIAN_POINT ( 'NONE',  ( 10.78501580275803562, -3.740707523384244837, 15.76143240460126371 ) ) ;
#109406=FACE_OUTER_BOUND ( 'NONE', #49059, .T. ) ;
#109407=CARTESIAN_POINT ( 'NONE',  ( -7.171830600776415210, -17.24070752338409918, 4.000000000000000000 ) ) ;
#109409=LINE ( 'NONE', #120991, #40413 ) ;
#109410=DIRECTION ( 'NONE',  ( 0.6830127018922180770, -0.6830127018922204085, -0.2588190451025213501 ) ) ;
#109411=DIRECTION ( 'NONE',  ( -0.000000000000000000, -0.3543493200069152693, 0.9351131265310292928 ) ) ;
#109412=VECTOR ( 'NONE', #66154, 1000.000000000000114 ) ;
#109413=VECTOR ( 'NONE', #47727, 1000.000000000000227 ) ;
#109414=CARTESIAN_POINT ( 'NONE',  ( -9.712309939660212166, -21.73547319004781642, 4.999917730833664642 ) ) ;
#109415=AXIS2_PLACEMENT_3D ( 'NONE', #55991, #22577, #67583 ) ;
#109416=AXIS2_PLACEMENT_3D ( 'NONE', #67730, #123532, #111167 ) ;
#109417=DIRECTION ( 'NONE',  ( -0.6830127018922180770, -0.6830127018922204085, -0.2588190451025213501 ) ) ;
#109418=CARTESIAN_POINT ( 'NONE',  ( -25.82816939922334853, 9.759292476615621936, 4.000000000000000000 ) ) ;
#109419=CARTESIAN_POINT ( 'NONE',  ( -26.20710678118635784, 0.7592924766157156391, 5.000000000000000000 ) ) ;
#109420=VERTEX_POINT ( 'NONE', #60139 ) ;
#109421=EDGE_LOOP ( 'NONE', ( #129175, #101251, #111845, #65063 ) ) ;
#109422=VECTOR ( 'NONE', #131460, 1000.000000000000227 ) ;
#109423=ORIENTED_EDGE ( 'NONE', *, *, #125688, .F. ) ;
#109424=VECTOR ( 'NONE', #15675, 1000.000000000000227 ) ;
#109425=CARTESIAN_POINT ( 'NONE',  ( 2.999999999999975131, -13.39766691384883224, -10.96608748226466545 ) ) ;
#109426=ORIENTED_EDGE ( 'NONE', *, *, #77385, .T. ) ;
#109427=ORIENTED_EDGE ( 'NONE', *, *, #55881, .F. ) ;
#109428=CARTESIAN_POINT ( 'NONE',  ( -54.18398860626899705, 28.73617430169825226, 5.000000000000000000 ) ) ;
#109429=LINE ( 'NONE', #12249, #133516 ) ;
#109430=DIRECTION ( 'NONE',  ( 0.7071067811865487940, 0.7071067811865463515, -0.000000000000000000 ) ) ;
#109431=VERTEX_POINT ( 'NONE', #106427 ) ;
#109433=ORIENTED_EDGE ( 'NONE', *, *, #20715, .T. ) ;
#109434=FACE_OUTER_BOUND ( 'NONE', #74926, .T. ) ;
#109436=VECTOR ( 'NONE', #114110, 1000.000000000000000 ) ;
#109438=EDGE_LOOP ( 'NONE', ( #65446, #1517, #8987, #75551 ) ) ;
#109440=EDGE_CURVE ( 'NONE', #107596, #75676, #82585, .T. ) ;
#109441=DIRECTION ( 'NONE',  ( 0.7071067811865486830, -0.7071067811865464625, -0.000000000000000000 ) ) ;
#109442=EDGE_CURVE ( 'NONE', #93231, #19799, #30340, .T. ) ;
#109443=PLANE ( 'NONE',  #25817 ) ;
#109444=CARTESIAN_POINT ( 'NONE',  ( -27.71230993966009493, -21.73547319004781642, 4.999917730833664642 ) ) ;
#109446=VERTEX_POINT ( 'NONE', #76732 ) ;
#109447=EDGE_CURVE ( 'NONE', #26808, #141246, #7643, .T. ) ;
#109448=ORIENTED_EDGE ( 'NONE', *, *, #65, .F. ) ;
#109449=PLANE ( 'NONE',  #92654 ) ;
#109450=LINE ( 'NONE', #133365, #67314 ) ;
#109451=LINE ( 'NONE', #98570, #49694 ) ;
#109452=ADVANCED_FACE ( 'NONE', ( #88308 ), #9251, .F. ) ;
#109453=PLANE ( 'NONE',  #79708 ) ;
#109455=VECTOR ( 'NONE', #100696, 1000.000000000000000 ) ;
#109456=LINE ( 'NONE', #32632, #34623 ) ;
#109458=EDGE_CURVE ( 'NONE', #36583, #93715, #54274, .T. ) ;
#109459=DIRECTION ( 'NONE',  ( -0.7071067811865487940, 0.7071067811865463515, 0.000000000000000000 ) ) ;
#109462=CARTESIAN_POINT ( 'NONE',  ( -14.81601139373099585, 28.73617430169776910, 5.000000000000000000 ) ) ;
#109464=VECTOR ( 'NONE', #18559, 999.9999999999998863 ) ;
#109465=DIRECTION ( 'NONE',  ( -0.7071067811865486830, 0.7071067811865464625, 0.000000000000000000 ) ) ;
#109466=EDGE_LOOP ( 'NONE', ( #91314, #96569, #10771, #138019 ) ) ;
#109468=CARTESIAN_POINT ( 'NONE',  ( -69.48921356237309510, -27.52281430457103895, 5.000000000000000000 ) ) ;
#109470=EDGE_LOOP ( 'NONE', ( #91078, #39922, #97761, #93036 ) ) ;
#109471=EDGE_CURVE ( 'NONE', #92475, #12567, #89031, .T. ) ;
#109472=LINE ( 'NONE', #9400, #47043 ) ;
#109473=DIRECTION ( 'NONE',  ( 0.7071067811865487940, 0.7071067811865463515, 0.000000000000000000 ) ) ;
#109474=ORIENTED_EDGE ( 'NONE', *, *, #60355, .F. ) ;
#109475=DIRECTION ( 'NONE',  ( 0.7071067811865487940, 0.7071067811865463515, -0.000000000000000000 ) ) ;
#109476=( BOUNDED_CURVE ( )  B_SPLINE_CURVE ( 3, ( #88851, #46807, #24974, #67085 ),
 .UNSPECIFIED., .F., .T. ) 
 B_SPLINE_CURVE_WITH_KNOTS ( ( 4, 4 ),
 ( 1.208578181583235045, 1.359146454359427825 ),
 .UNSPECIFIED. ) 
 CURVE ( )  GEOMETRIC_REPRESENTATION_ITEM ( )  RATIONAL_B_SPLINE_CURVE ( ( 1.000000000000000000, 0.9981116584018955296, 0.9981116584018955296, 1.000000000000000000 ) ) 
 REPRESENTATION_ITEM ( '' )  );
#109477=EDGE_CURVE ( 'NONE', #102386, #111653, #100610, .T. ) ;
#109479=LINE ( 'NONE', #118179, #112360 ) ;
#109481=CARTESIAN_POINT ( 'NONE',  ( -9.005480084712511157, 28.92564299267931816, 4.000000000000000000 ) ) ;
#109483=FACE_OUTER_BOUND ( 'NONE', #20131, .T. ) ;
#109484=FACE_OUTER_BOUND ( 'NONE', #43388, .T. ) ;
#109485=DIRECTION ( 'NONE',  ( -0.7071067811865486830, 0.7071067811865464625, 0.000000000000000000 ) ) ;
#109486=CARTESIAN_POINT ( 'NONE',  ( -2.999999999999975131, -19.06887692260761469, 4.000000000000000000 ) ) ;
#109487=CARTESIAN_POINT ( 'NONE',  ( -48.18398860626899705, 28.73617430169820608, 5.000000000000000000 ) ) ;
#109488=VECTOR ( 'NONE', #134133, 1000.000000000000000 ) ;
#109489=LINE ( 'NONE', #54427, #20566 ) ;
#109491=LINE ( 'NONE', #75448, #45452 ) ;
#109496=EDGE_LOOP ( 'NONE', ( #7221, #58979, #10857, #124107 ) ) ;
#109497=VERTEX_POINT ( 'NONE', #135396 ) ;
#109498=ORIENTED_EDGE ( 'NONE', *, *, #30459, .T. ) ;
#109499=ADVANCED_FACE ( 'NONE', ( #58582 ), #125207, .F. ) ;
#109500=DIRECTION ( 'NONE',  ( 1.000000000000000000, 0.000000000000000000, 0.000000000000000000 ) ) ;
#109502=AXIS2_PLACEMENT_3D ( 'NONE', #108434, #141088, #87457 ) ;
#109504=LINE ( 'NONE', #142849, #4575 ) ;
#109505=FACE_OUTER_BOUND ( 'NONE', #116346, .T. ) ;
#109506=PLANE ( 'NONE',  #97302 ) ;
#109508=ORIENTED_EDGE ( 'NONE', *, *, #137605, .F. ) ;
#109510=CARTESIAN_POINT ( 'NONE',  ( -8.510786437626906675, -27.52281430457049183, 5.000000000000000000 ) ) ;
#109512=LINE ( 'NONE', #9448, #130818 ) ;
#109513=FACE_OUTER_BOUND ( 'NONE', #125187, .T. ) ;
#109516=EDGE_CURVE ( 'NONE', #48278, #22430, #122318, .T. ) ;
#109517=LINE ( 'NONE', #22476, #120945 ) ;
#109518=ORIENTED_EDGE ( 'NONE', *, *, #23688, .T. ) ;
#109521=VERTEX_POINT ( 'NONE', #114320 ) ;
#109523=EDGE_CURVE ( 'NONE', #90471, #19069, #22992, .T. ) ;
#109524=CARTESIAN_POINT ( 'NONE',  ( -60.48921356237309510, -27.52281430457097500, 5.000000000000000000 ) ) ;
#109525=VECTOR ( 'NONE', #60843, 1000.000000000000000 ) ;
#109526=DIRECTION ( 'NONE',  ( 0.6830127018922181881, 0.6830127018922202975, -0.2588190451025214056 ) ) ;
#109528=DIRECTION ( 'NONE',  ( 0.6830127018922181881, 0.6830127018922202975, -0.2588190451025214056 ) ) ;
#109530=AXIS2_PLACEMENT_3D ( 'NONE', #6484, #138493, #84138 ) ;
#109533=EDGE_CURVE ( 'NONE', #16928, #76456, #13557, .T. ) ;
#109535=AXIS2_PLACEMENT_3D ( 'NONE', #16067, #94373, #28432 ) ;
#109536=CARTESIAN_POINT ( 'NONE',  ( -28.49999999999979750, -12.66682484999668468, -0.6294897503864617105 ) ) ;
#109537=CARTESIAN_POINT ( 'NONE',  ( 26.50183651486027969, -17.24070752338409918, 8.407044977365165650 ) ) ;
#109538=VERTEX_POINT ( 'NONE', #23756 ) ;
#109540=ADVANCED_FACE ( 'NONE', ( #14996 ), #25161, .T. ) ;
#109541=ORIENTED_EDGE ( 'NONE', *, *, #83391, .T. ) ;
#109542=DIRECTION ( 'NONE',  ( -0.000000000000000000, 0.000000000000000000, 1.000000000000000000 ) ) ;
#109543=CARTESIAN_POINT ( 'NONE',  ( -22.21498419724176188, -3.740707523384238176, 15.76143240460118733 ) ) ;
#109544=VECTOR ( 'NONE', #17625, 1000.000000000000000 ) ;
#109547=CARTESIAN_POINT ( 'NONE',  ( -22.49999999999984013, -12.08601207473290451, -10.46905243149088705 ) ) ;
#109548=ORIENTED_EDGE ( 'NONE', *, *, #76213, .F. ) ;
#109549=EDGE_LOOP ( 'NONE', ( #79340, #124612, #94456, #140370 ) ) ;
#109550=ORIENTED_EDGE ( 'NONE', *, *, #75617, .T. ) ;
#109551=VECTOR ( 'NONE', #38831, 999.9999999999998863 ) ;
#109552=CARTESIAN_POINT ( 'NONE',  ( -24.18398860626899705, 28.73617430169804265, 5.000000000000000000 ) ) ;
#109554=DIRECTION ( 'NONE',  ( 0.7071067811865487940, 0.7071067811865463515, 0.000000000000000000 ) ) ;
#109555=ADVANCED_FACE ( 'NONE', ( #133249 ), #12148, .F. ) ;
#109556=VERTEX_POINT ( 'NONE', #36756 ) ;
#109557=VECTOR ( 'NONE', #76302, 1000.000000000000000 ) ;
#109560=CARTESIAN_POINT ( 'NONE',  ( -8.671830600776406328, -3.740707523384244837, 4.000000000000000000 ) ) ;
#109561=VECTOR ( 'NONE', #64175, 1000.000000000000000 ) ;
#109562=EDGE_CURVE ( 'NONE', #102959, #110646, #56430, .T. ) ;
#109563=FACE_BOUND ( 'NONE', #137107, .T. ) ;
#109564=ORIENTED_EDGE ( 'NONE', *, *, #131094, .T. ) ;
#109565=FACE_OUTER_BOUND ( 'NONE', #69117, .T. ) ;
#109568=VERTEX_POINT ( 'NONE', #4071 ) ;
#109570=VERTEX_POINT ( 'NONE', #119824 ) ;
#109571=ORIENTED_EDGE ( 'NONE', *, *, #45421, .F. ) ;
#109573=AXIS2_PLACEMENT_3D ( 'NONE', #136667, #104762, #103312 ) ;
#109575=VECTOR ( 'NONE', #11912, 1000.000000000000000 ) ;
#109576=VERTEX_POINT ( 'NONE', #73009 ) ;
#109577=DIRECTION ( 'NONE',  ( 0.7071067811865487940, 0.7071067811865463515, 0.000000000000000000 ) ) ;
#109579=CARTESIAN_POINT ( 'NONE',  ( 25.49999999999982236, 10.94296225409029510, -9.576120664313199526 ) ) ;
#109580=ORIENTED_EDGE ( 'NONE', *, *, #91262, .F. ) ;
#109582=DIRECTION ( 'NONE',  ( -0.000000000000000000, -0.3543493200069152693, 0.9351131265310292928 ) ) ;
#109584=ADVANCED_FACE ( 'NONE', ( #81737 ), #137518, .F. ) ;
#109585=LINE ( 'NONE', #10261, #10776 ) ;
#109588=LINE ( 'NONE', #140105, #139677 ) ;
#109589=CARTESIAN_POINT ( 'NONE',  ( 28.49999999999980460, 21.05218569542895324, 5.000000000000000000 ) ) ;
#109590=ORIENTED_EDGE ( 'NONE', *, *, #23529, .T. ) ;
#109592=ORIENTED_EDGE ( 'NONE', *, *, #94668, .F. ) ;
#109593=EDGE_LOOP ( 'NONE', ( #90613, #63843, #130969, #1677 ) ) ;
#109594=DIRECTION ( 'NONE',  ( -0.7071067811865486830, 0.7071067811865464625, 0.000000000000000000 ) ) ;
#109595=CARTESIAN_POINT ( 'NONE',  ( 35.99451991528749772, 28.92564299267963079, 4.000000000000000000 ) ) ;
#109596=ORIENTED_EDGE ( 'NONE', *, *, #19759, .F. ) ;
#109597=ORIENTED_EDGE ( 'NONE', *, *, #29745, .T. ) ;
#109598=DIRECTION ( 'NONE',  ( -0.000000000000000000, 1.000000000000000000, -0.000000000000000000 ) ) ;
#109599=PLANE ( 'NONE',  #38719 ) ;
#109601=VERTEX_POINT ( 'NONE', #59963 ) ;
#109605=EDGE_CURVE ( 'NONE', #74842, #59437, #6228, .T. ) ;
#109606=VECTOR ( 'NONE', #96198, 1000.000000000000000 ) ;
#109607=DIRECTION ( 'NONE',  ( -0.6830127018922180770, -0.6830127018922204085, -0.2588190451025213501 ) ) ;
#109608=ORIENTED_EDGE ( 'NONE', *, *, #136078, .T. ) ;
#109610=EDGE_CURVE ( 'NONE', #17066, #89804, #50504, .T. ) ;
#109611=CARTESIAN_POINT ( 'NONE',  ( -34.92500000000001137, 22.22500000000000142, 4.500000000000000888 ) ) ;
#109613=DIRECTION ( 'NONE',  ( 0.7071067811865487940, 0.7071067811865463515, -0.000000000000000000 ) ) ;
#109614=ORIENTED_EDGE ( 'NONE', *, *, #89886, .F. ) ;
#109615=LINE ( 'NONE', #63306, #81003 ) ;
#109616=ORIENTED_EDGE ( 'NONE', *, *, #101594, .F. ) ;
#109617=LINE ( 'NONE', #130691, #89009 ) ;
#109618=LINE ( 'NONE', #44406, #125687 ) ;
#109619=ADVANCED_FACE ( 'NONE', ( #61425 ), #39653, .T. ) ;
#109620=EDGE_CURVE ( 'NONE', #73002, #75311, #94690, .T. ) ;
#109622=AXIS2_PLACEMENT_3D ( 'NONE', #37766, #103005, #3638 ) ;
#109623=VERTEX_POINT ( 'NONE', #49816 ) ;
#109624=DIRECTION ( 'NONE',  ( -0.7071067811865486830, 0.7071067811865464625, 0.000000000000000000 ) ) ;
#109625=DIRECTION ( 'NONE',  ( 0.7071067811865487940, 0.7071067811865463515, -0.000000000000000000 ) ) ;
#109626=ORIENTED_EDGE ( 'NONE', *, *, #73623, .T. ) ;
#109628=DIRECTION ( 'NONE',  ( -0.6830127018922181881, 0.6830127018922202975, -0.2588190451025214056 ) ) ;
#109629=CARTESIAN_POINT ( 'NONE',  ( -42.18398860626899705, 28.73617430169816700, 5.000000000000000000 ) ) ;
#109630=VERTEX_POINT ( 'NONE', #138223 ) ;
#109631=EDGE_CURVE ( 'NONE', #41654, #140719, #92545, .T. ) ;
#109632=LINE ( 'NONE', #141567, #108631 ) ;
#109633=DIRECTION ( 'NONE',  ( 0.6830127018922180770, -0.6830127018922204085, -0.2588190451025213501 ) ) ;
#109634=ORIENTED_EDGE ( 'NONE', *, *, #60366, .T. ) ;
#109635=EDGE_CURVE ( 'NONE', #6599, #97151, #128083, .T. ) ;
#109637=VERTEX_POINT ( 'NONE', #38909 ) ;
#109638=PLANE ( 'NONE',  #17163 ) ;
#109640=AXIS2_PLACEMENT_3D ( 'NONE', #51296, #92618, #17219 ) ;
#109641=VERTEX_POINT ( 'NONE', #138949 ) ;
#109642=EDGE_CURVE ( 'NONE', #141613, #36536, #15676, .T. ) ;
#109643=DIRECTION ( 'NONE',  ( 0.7071067811865487940, 0.7071067811865463515, -0.000000000000000000 ) ) ;
#109644=AXIS2_PLACEMENT_3D ( 'NONE', #10161, #76891, #79037 ) ;
#109645=LINE ( 'NONE', #108183, #62182 ) ;
#109646=CARTESIAN_POINT ( 'NONE',  ( 31.49999999999978684, 7.087461875839177416, 4.000000000000000000 ) ) ;
#109647=ORIENTED_EDGE ( 'NONE', *, *, #64823, .F. ) ;
#109648=PLANE ( 'NONE',  #123041 ) ;
#109649=CARTESIAN_POINT ( 'NONE',  ( -48.48921356237309510, -27.52281430457089328, 5.000000000000000000 ) ) ;
#109650=CARTESIAN_POINT ( 'NONE',  ( 5.510786437626906675, -27.52281430457051314, 5.000000000000000000 ) ) ;
#109651=EDGE_CURVE ( 'NONE', #25131, #33645, #106267, .T. ) ;
#109652=CARTESIAN_POINT ( 'NONE',  ( 5.999999999999958256, -16.60178936734448030, 0.8616154019347637139 ) ) ;
#109654=AXIS2_PLACEMENT_3D ( 'NONE', #114070, #14024, #3155 ) ;
#109655=DIRECTION ( 'NONE',  ( 0.6830127018922180770, -0.6830127018922204085, -0.2588190451025213501 ) ) ;
#109656=ORIENTED_EDGE ( 'NONE', *, *, #113914, .F. ) ;
#109657=ORIENTED_EDGE ( 'NONE', *, *, #112766, .T. ) ;
#109658=DIRECTION ( 'NONE',  ( -0.7071067811865487940, 0.7071067811865463515, -0.000000000000000000 ) ) ;
#109660=ORIENTED_EDGE ( 'NONE', *, *, #34511, .T. ) ;
#109661=ORIENTED_EDGE ( 'NONE', *, *, #96015, .T. ) ;
#109662=ADVANCED_FACE ( 'NONE', ( #6941 ), #82422, .F. ) ;
#109663=CARTESIAN_POINT ( 'NONE',  ( -23.99999999999982236, -9.412538124160663600, 4.000000000000000000 ) ) ;
#109664=LINE ( 'NONE', #98771, #27706 ) ;
#109667=VECTOR ( 'NONE', #94217, 1000.000000000000000 ) ;
#109668=CARTESIAN_POINT ( 'NONE',  ( -13.64175702458852335, 15.75929247661555799, 19.34181609438702765 ) ) ;
#109669=CARTESIAN_POINT ( 'NONE',  ( -39.48921356237310221, -27.52281430457082934, 5.000000000000000000 ) ) ;
#109670=CARTESIAN_POINT ( 'NONE',  ( 34.49999999999975131, -20.94567065516883630, 4.994342998332155226 ) ) ;
#109671=ORIENTED_EDGE ( 'NONE', *, *, #4152, .T. ) ;
#109672=ADVANCED_FACE ( 'NONE', ( #4792 ), #40367, .F. ) ;
#109673=DIRECTION ( 'NONE',  ( 0.6830127018922180770, -0.6830127018922204085, -0.2588190451025213501 ) ) ;
#109674=FACE_OUTER_BOUND ( 'NONE', #71058, .T. ) ;
#109675=EDGE_CURVE ( 'NONE', #79378, #110593, #130763, .T. ) ;
#109676=PLANE ( 'NONE',  #56622 ) ;
#109677=VECTOR ( 'NONE', #123757, 999.9999999999998863 ) ;
#109680=DIRECTION ( 'NONE',  ( 0.7071067811865487940, -0.7071067811865463515, 0.000000000000000000 ) ) ;
#109682=AXIS2_PLACEMENT_3D ( 'NONE', #63787, #139212, #39904 ) ;
#109685=DIRECTION ( 'NONE',  ( -0.7071067811865487940, 0.7071067811865463515, 0.000000000000000000 ) ) ;
#109686=AXIS2_PLACEMENT_3D ( 'NONE', #76090, #1350, #54371 ) ;
#109687=CARTESIAN_POINT ( 'NONE',  ( 21.18398860626899349, 28.73617430169802134, 5.000000000000000000 ) ) ;
#109688=ORIENTED_EDGE ( 'NONE', *, *, #124422, .F. ) ;
#109689=VERTEX_POINT ( 'NONE', #48356 ) ;
#109691=FACE_OUTER_BOUND ( 'NONE', #8756, .T. ) ;
#109692=VECTOR ( 'NONE', #4043, 1000.000000000000000 ) ;
#109694=CARTESIAN_POINT ( 'NONE',  ( -17.99999999999987210, -11.35517001088073563, -1.126524801160152300 ) ) ;
#109696=CARTESIAN_POINT ( 'NONE',  ( 0.000000000000000000, 0.000000000000000000, 5.000000000000000000 ) ) ;
#109698=ORIENTED_EDGE ( 'NONE', *, *, #96621, .T. ) ;
#109700=EDGE_LOOP ( 'NONE', ( #39106, #123428, #98148, #10807 ) ) ;
#109701=ORIENTED_EDGE ( 'NONE', *, *, #39296, .T. ) ;
#109702=AXIS2_PLACEMENT_3D ( 'NONE', #77208, #19923, #99620 ) ;
#109703=LINE ( 'NONE', #132923, #104806 ) ;
#109704=CARTESIAN_POINT ( 'NONE',  ( 18.38945826904184599, 9.109118024354394549, 4.348864708961791337 ) ) ;
#109705=DIRECTION ( 'NONE',  ( 0.3543493200069162685, -0.000000000000000000, -0.9351131265310288487 ) ) ;
#109706=FACE_OUTER_BOUND ( 'NONE', #52089, .T. ) ;
#109707=ORIENTED_EDGE ( 'NONE', *, *, #133729, .F. ) ;
#109708=CARTESIAN_POINT ( 'NONE',  ( 51.29974487139158867, -27.71228299555242103, 4.000000000000000000 ) ) ;
#109710=ORIENTED_EDGE ( 'NONE', *, *, #71330, .T. ) ;
#109713=DIRECTION ( 'NONE',  ( 0.6830127018922180770, -0.6830127018922204085, -0.2588190451025213501 ) ) ;
#109714=DIRECTION ( 'NONE',  ( -0.7071067811865487940, 0.7071067811865463515, -0.000000000000000000 ) ) ;
#109715=CARTESIAN_POINT ( 'NONE',  ( -11.28242261357426379, -21.73023691814493930, 5.000000000000000888 ) ) ;
#109716=CARTESIAN_POINT ( 'NONE',  ( 34.92499999999998295, 19.70193056682078137, 4.500000000000000888 ) ) ;
#109717=ORIENTED_EDGE ( 'NONE', *, *, #116696, .T. ) ;
#109719=LINE ( 'NONE', #132214, #110137 ) ;
#109721=CARTESIAN_POINT ( 'NONE',  ( 17.70025512860841488, -27.71228299555193786, 4.000000000000000000 ) ) ;
#109722=CARTESIAN_POINT ( 'NONE',  ( 39.18398860626899705, 28.73617430169814568, 5.000000000000000000 ) ) ;
#109724=VERTEX_POINT ( 'NONE', #125930 ) ;
#109725=ORIENTED_EDGE ( 'NONE', *, *, #140510, .T. ) ;
#109726=DIRECTION ( 'NONE',  ( 0.6830127018922181881, 0.6830127018922202975, -0.2588190451025214056 ) ) ;
#109728=ORIENTED_EDGE ( 'NONE', *, *, #96784, .F. ) ;
#109729=VECTOR ( 'NONE', #2758, 1000.000000000000000 ) ;
#109730=ORIENTED_EDGE ( 'NONE', *, *, #103956, .T. ) ;
#109731=CARTESIAN_POINT ( 'NONE',  ( -27.47512612785028807, 14.25929247661557042, 9.797011795316574734 ) ) ;
#109732=ORIENTED_EDGE ( 'NONE', *, *, #6308, .F. ) ;
#109734=FACE_OUTER_BOUND ( 'NONE', #44054, .T. ) ;
#109735=CARTESIAN_POINT ( 'NONE',  ( 13.49999999999990408, -10.04351517176476882, -1.623559851933791931 ) ) ;
#109736=ADVANCED_FACE ( 'NONE', ( #26604 ), #70847, .F. ) ;
#109737=FACE_BOUND ( 'NONE', #7543, .T. ) ;
#109738=DIRECTION ( 'NONE',  ( -0.6830127018922180770, -0.6830127018922204085, -0.2588190451025213501 ) ) ;
#109740=EDGE_CURVE ( 'NONE', #13955, #4377, #100255, .T. ) ;
#109741=PLANE ( 'NONE',  #15553 ) ;
#109742=FACE_OUTER_BOUND ( 'NONE', #42179, .T. ) ;
#109743=ORIENTED_EDGE ( 'NONE', *, *, #9311, .T. ) ;
#109744=VECTOR ( 'NONE', #29340, 1000.000000000000227 ) ;
#109745=PLANE ( 'NONE',  #92602 ) ;
#109747=VECTOR ( 'NONE', #22268, 1000.000000000000000 ) ;
#109748=ORIENTED_EDGE ( 'NONE', *, *, #78055, .F. ) ;
#109750=ORIENTED_EDGE ( 'NONE', *, *, #66270, .T. ) ;
#109751=CARTESIAN_POINT ( 'NONE',  ( 20.99999999999985434, 15.45873954670187089, -0.03131636524298948149 ) ) ;
#109753=DIRECTION ( 'NONE',  ( 0.7071067811865487940, 0.7071067811865463515, 0.000000000000000000 ) ) ;
#109754=ORIENTED_EDGE ( 'NONE', *, *, #93745, .F. ) ;
#109755=PLANE ( 'NONE',  #127817 ) ;
#109756=EDGE_CURVE ( 'NONE', #48818, #38475, #56793, .T. ) ;
#109757=CARTESIAN_POINT ( 'NONE',  ( 21.15612307739225884, -22.22499999999999432, 4.000000000000000000 ) ) ;
#109758=LINE ( 'NONE', #69681, #9003 ) ;
#109759=LINE ( 'NONE', #140949, #38556 ) ;
#109760=VECTOR ( 'NONE', #34058, 1000.000000000000000 ) ;
#109761=CARTESIAN_POINT ( 'NONE',  ( -60.18398860626900415, 28.73617430169829490, 5.000000000000000000 ) ) ;
#109762=DIRECTION ( 'NONE',  ( -0.3543493200069162685, -0.000000000000000000, -0.9351131265310288487 ) ) ;
#109763=FACE_OUTER_BOUND ( 'NONE', #94212, .T. ) ;
#109764=DIRECTION ( 'NONE',  ( 0.7071067811865487940, -0.7071067811865463515, 0.000000000000000000 ) ) ;
#109765=EDGE_LOOP ( 'NONE', ( #116734, #46355, #120674, #71159 ) ) ;
#109766=EDGE_CURVE ( 'NONE', #6851, #23129, #90069, .T. ) ;
#109768=ORIENTED_EDGE ( 'NONE', *, *, #113374, .F. ) ;
#109772=ORIENTED_EDGE ( 'NONE', *, *, #48164, .F. ) ;
#109773=ORIENTED_EDGE ( 'NONE', *, *, #44593, .T. ) ;
#109774=VECTOR ( 'NONE', #133523, 999.9999999999998863 ) ;
#109776=ORIENTED_EDGE ( 'NONE', *, *, #67832, .F. ) ;
#109777=LINE ( 'NONE', #96720, #101426 ) ;
#109779=CARTESIAN_POINT ( 'NONE',  ( -27.48921356237309155, -27.52281430457074762, 5.000000000000000000 ) ) ;
#109783=ORIENTED_EDGE ( 'NONE', *, *, #137302, .T. ) ;
#109785=EDGE_CURVE ( 'NONE', #73824, #80946, #111849, .T. ) ;
#109786=ORIENTED_EDGE ( 'NONE', *, *, #47240, .T. ) ;
#109787=CARTESIAN_POINT ( 'NONE',  ( 36.29974487139159578, -27.71228299555231445, 4.000000000000000000 ) ) ;
#109789=DIRECTION ( 'NONE',  ( 1.000000000000000000, 0.000000000000000000, 0.000000000000000000 ) ) ;
#109790=EDGE_LOOP ( 'NONE', ( #80570, #100454, #19148, #89736 ) ) ;
#109791=ORIENTED_EDGE ( 'NONE', *, *, #136069, .F. ) ;
#109792=DIRECTION ( 'NONE',  ( 0.6830127018922180770, -0.6830127018922204085, -0.2588190451025213501 ) ) ;
#109793=CARTESIAN_POINT ( 'NONE',  ( 26.99999999999981526, 4.384688058510593400, -7.090945410444622787 ) ) ;
#109795=EDGE_CURVE ( 'NONE', #126646, #64188, #98114, .T. ) ;
#109796=LINE ( 'NONE', #86640, #88787 ) ;
#109797=ORIENTED_EDGE ( 'NONE', *, *, #24362, .T. ) ;
#109798=DIRECTION ( 'NONE',  ( 0.7071067811865486830, -0.7071067811865464625, -0.000000000000000000 ) ) ;
#109799=EDGE_LOOP ( 'NONE', ( #68565, #24938, #139458, #37385 ) ) ;
#109802=CARTESIAN_POINT ( 'NONE',  ( 34.22674160717812697, -11.24070752338416490, 18.24660765846990529 ) ) ;
#109803=VECTOR ( 'NONE', #100725, 999.9999999999998863 ) ;
#109804=PLANE ( 'NONE',  #55462 ) ;
#109805=ADVANCED_FACE ( 'NONE', ( #89373 ), #142343, .F. ) ;
#109807=DIRECTION ( 'NONE',  ( 0.7071067811865487940, 0.7071067811865463515, 0.000000000000000000 ) ) ;
#109808=CARTESIAN_POINT ( 'NONE',  ( -10.49999999999992006, -1.912538124160735542, 4.000000000000000000 ) ) ;
#109810=DIRECTION ( 'NONE',  ( -0.7071067811865486830, -0.7071067811865464625, -0.000000000000000000 ) ) ;
#109811=ORIENTED_EDGE ( 'NONE', *, *, #30382, .T. ) ;
#109812=ADVANCED_FACE ( 'NONE', ( #23387 ), #65518, .F. ) ;
#109814=ORIENTED_EDGE ( 'NONE', *, *, #36611, .T. ) ;
#109815=CARTESIAN_POINT ( 'NONE',  ( -27.48921356237309155, -27.52281430457074762, 5.000000000000000000 ) ) ;
#109817=CARTESIAN_POINT ( 'NONE',  ( 34.92499999999998295, 16.70193056682081334, 4.500000000000000888 ) ) ;
#109818=EDGE_LOOP ( 'NONE', ( #141440, #73627, #17382, #75378 ) ) ;
#109819=CARTESIAN_POINT ( 'NONE',  ( 7.499999999999954703, -8.947814304570741228, 5.000000000000000000 ) ) ;
#109820=CARTESIAN_POINT ( 'NONE',  ( 54.48921356237310221, -27.52281430457093236, 5.000000000000000000 ) ) ;
#109821=ADVANCED_FACE ( 'NONE', ( #121279 ), #77795, .F. ) ;
#109824=EDGE_LOOP ( 'NONE', ( #30077, #3578, #71453, #16281 ) ) ;
#109825=PLANE ( 'NONE',  #2448 ) ;
#109826=CARTESIAN_POINT ( 'NONE',  ( 39.48921356237310221, -27.52281430457082934, 5.000000000000000000 ) ) ;
#109827=LINE ( 'NONE', #45325, #5214 ) ;
#109828=EDGE_CURVE ( 'NONE', #122500, #77801, #100952, .T. ) ;
#109829=DIRECTION ( 'NONE',  ( 0.6830127018922181881, 0.6830127018922202975, -0.2588190451025214056 ) ) ;
#109832=DIRECTION ( 'NONE',  ( 0.7071067811865487940, 0.7071067811865463515, -0.000000000000000000 ) ) ;
#109833=CARTESIAN_POINT ( 'NONE',  ( -19.49999999999986500, 18.05218569542898521, 5.000000000000000000 ) ) ;
#109835=ORIENTED_EDGE ( 'NONE', *, *, #64823, .T. ) ;
#109837=ORIENTED_EDGE ( 'NONE', *, *, #59328, .T. ) ;
#109838=FACE_OUTER_BOUND ( 'NONE', #121429, .T. ) ;
#109839=LINE ( 'NONE', #41016, #17472 ) ;
#109840=DIRECTION ( 'NONE',  ( 1.000000000000000000, 0.000000000000000000, 0.000000000000000000 ) ) ;
#109842=DIRECTION ( 'NONE',  ( -0.7071067811865487940, -0.7071067811865463515, -0.000000000000000000 ) ) ;
#109843=CARTESIAN_POINT ( 'NONE',  ( -31.49999999999978684, 11.52377502935400955, -1.522421517564011006 ) ) ;
#109844=CARTESIAN_POINT ( 'NONE',  ( 69.48921356237309510, -27.52281430457103895, 5.000000000000000000 ) ) ;
#109845=VERTEX_POINT ( 'NONE', #21963 ) ;
#109846=EDGE_LOOP ( 'NONE', ( #133336, #84620, #22510, #50472 ) ) ;
#109847=CARTESIAN_POINT ( 'NONE',  ( -57.18398860626899705, 28.73617430169827358, 5.000000000000000000 ) ) ;
#109848=PLANE ( 'NONE',  #18986 ) ;
#109852=DIRECTION ( 'NONE',  ( -0.7071067811865486830, -0.7071067811865464625, 0.000000000000000000 ) ) ;
#109853=ADVANCED_FACE ( 'NONE', ( #98803 ), #66209, .F. ) ;
#109855=CARTESIAN_POINT ( 'NONE',  ( -31.49999999999977973, 10.94296225409023826, -9.576120664313327424 ) ) ;
#109856=EDGE_CURVE ( 'NONE', #74581, #23590, #87941, .T. ) ;
#109857=AXIS2_PLACEMENT_3D ( 'NONE', #4242, #93470, #137705 ) ;
#109858=ORIENTED_EDGE ( 'NONE', *, *, #38594, .T. ) ;
#109861=AXIS2_PLACEMENT_3D ( 'NONE', #23555, #11212, #88111 ) ;
#109862=CARTESIAN_POINT ( 'NONE',  ( -25.80981832425536027, -18.74070752338408852, 7.910009926591568430 ) ) ;
#109863=DIRECTION ( 'NONE',  ( 0.7071067811865487940, 0.7071067811865463515, 0.000000000000000000 ) ) ;
#109864=ORIENTED_EDGE ( 'NONE', *, *, #116490, .T. ) ;
#109865=EDGE_CURVE ( 'NONE', #128485, #60505, #92940, .T. ) ;
#109869=VECTOR ( 'NONE', #35760, 1000.000000000000000 ) ;
#109871=LINE ( 'NONE', #43207, #73209 ) ;
#109872=ORIENTED_EDGE ( 'NONE', *, *, #108774, .F. ) ;
#109873=DIRECTION ( 'NONE',  ( 0.7071067811865487940, -0.7071067811865463515, 0.000000000000000000 ) ) ;
#109874=FACE_OUTER_BOUND ( 'NONE', #122613, .T. ) ;
#109875=LINE ( 'NONE', #118604, #34965 ) ;
#109876=DIRECTION ( 'NONE',  ( -0.000000000000000000, 0.3543493200069153248, 0.9351131265310292928 ) ) ;
#109878=DIRECTION ( 'NONE',  ( 1.000000000000000000, 0.000000000000000000, 0.000000000000000000 ) ) ;
#109879=ORIENTED_EDGE ( 'NONE', *, *, #39331, .F. ) ;
#109880=PLANE ( 'NONE',  #60025 ) ;
#109881=LINE ( 'NONE', #124326, #52235 ) ;
#109882=FACE_OUTER_BOUND ( 'NONE', #101910, .T. ) ;
#109883=( BOUNDED_CURVE ( )  B_SPLINE_CURVE ( 3, ( #1748, #113396, #14080, #2476 ),
 .UNSPECIFIED., .F., .F. ) 
 B_SPLINE_CURVE_WITH_KNOTS ( ( 4, 4 ),
 ( 5.005968288816728062, 5.074607125596347856 ),
 .UNSPECIFIED. ) 
 CURVE ( )  GEOMETRIC_REPRESENTATION_ITEM ( )  RATIONAL_B_SPLINE_CURVE ( ( 1.000000000000000000, 0.9996074310407763175, 0.9996074310407763175, 1.000000000000000000 ) ) 
 REPRESENTATION_ITEM ( '' )  );
#109884=DIRECTION ( 'NONE',  ( -1.000000000000000000, 0.000000000000000000, 0.000000000000000000 ) ) ;
#109885=VECTOR ( 'NONE', #42445, 1000.000000000000000 ) ;
#109886=ORIENTED_EDGE ( 'NONE', *, *, #14812, .T. ) ;
#109887=ORIENTED_EDGE ( 'NONE', *, *, #89796, .F. ) ;
#109889=VECTOR ( 'NONE', #46305, 999.9999999999998863 ) ;
#109890=VECTOR ( 'NONE', #4184, 1000.000000000000000 ) ;
#109891=ORIENTED_EDGE ( 'NONE', *, *, #129751, .F. ) ;
#109893=CARTESIAN_POINT ( 'NONE',  ( -34.92500000000001137, -22.22500000000000142, 4.000000000000000000 ) ) ;
#109894=DIRECTION ( 'NONE',  ( -0.000000000000000000, -0.3543493200069152693, 0.9351131265310292928 ) ) ;
#109895=EDGE_CURVE ( 'NONE', #26574, #141092, #92208, .T. ) ;
#109896=DIRECTION ( 'NONE',  ( -0.000000000000000000, 0.000000000000000000, 1.000000000000000000 ) ) ;
#109897=VERTEX_POINT ( 'NONE', #25531 ) ;
#109898=ORIENTED_EDGE ( 'NONE', *, *, #56857, .F. ) ;
#109899=CARTESIAN_POINT ( 'NONE',  ( 0.000000000000000000, 0.000000000000000000, 5.000000000000000000 ) ) ;
#109901=ORIENTED_EDGE ( 'NONE', *, *, #64445, .T. ) ;
#109902=DIRECTION ( 'NONE',  ( 0.7071067811865486830, -0.7071067811865464625, -0.000000000000000000 ) ) ;
#109903=DIRECTION ( 'NONE',  ( 0.6830127018922180770, -0.6830127018922204085, -0.2588190451025213501 ) ) ;
#109904=CARTESIAN_POINT ( 'NONE',  ( -8.010880286539427075, -22.02621442084248216, 4.990779571109221990 ) ) ;
#109905=EDGE_LOOP ( 'NONE', ( #14207, #6874, #31506, #92288 ) ) ;
#109906=EDGE_CURVE ( 'NONE', #129514, #49064, #3748, .T. ) ;
#109907=EDGE_CURVE ( 'NONE', #49712, #97236, #57486, .T. ) ;
#109908=FACE_BOUND ( 'NONE', #83879, .T. ) ;
#109911=LINE ( 'NONE', #22868, #69109 ) ;
#109913=ADVANCED_FACE ( 'NONE', ( #112553 ), #113981, .F. ) ;
#109915=FACE_OUTER_BOUND ( 'NONE', #132409, .T. ) ;
#109916=VERTEX_POINT ( 'NONE', #35752 ) ;
#109917=ORIENTED_EDGE ( 'NONE', *, *, #4857, .T. ) ;
#109919=ORIENTED_EDGE ( 'NONE', *, *, #34944, .F. ) ;
#109920=EDGE_CURVE ( 'NONE', #75431, #131861, #48036, .T. ) ;
#109921=ORIENTED_EDGE ( 'NONE', *, *, #105147, .F. ) ;
#109923=VECTOR ( 'NONE', #116722, 999.9999999999998863 ) ;
#109924=ADVANCED_FACE ( 'NONE', ( #59633 ), #136434, .F. ) ;
#109925=FACE_OUTER_BOUND ( 'NONE', #39408, .T. ) ;
#109927=DIRECTION ( 'NONE',  ( 0.3543493200069162685, -0.000000000000000000, -0.9351131265310288487 ) ) ;
#109928=DIRECTION ( 'NONE',  ( 0.6830127018922181881, 0.6830127018922202975, -0.2588190451025214056 ) ) ;
#109929=DIRECTION ( 'NONE',  ( -0.6830127018922181881, 0.6830127018922202975, -0.2588190451025214056 ) ) ;
#109931=ADVANCED_FACE ( 'NONE', ( #124854 ), #126287, .F. ) ;
#109932=CARTESIAN_POINT ( 'NONE',  ( -8.994519915287490619, 28.92564299267944250, 4.000000000000000000 ) ) ;
#109934=LINE ( 'NONE', #20052, #60665 ) ;
#109935=ORIENTED_EDGE ( 'NONE', *, *, #12077, .T. ) ;
#109936=DIRECTION ( 'NONE',  ( -0.3543493200069162685, -0.000000000000000000, -0.9351131265310288487 ) ) ;
#109937=DIRECTION ( 'NONE',  ( -0.7071067811865486830, -0.7071067811865464625, 0.000000000000000000 ) ) ;
#109940=VERTEX_POINT ( 'NONE', #103788 ) ;
#109942=EDGE_CURVE ( 'NONE', #8318, #141462, #90826, .T. ) ;
#109943=ORIENTED_EDGE ( 'NONE', *, *, #105935, .F. ) ;
#109944=DIRECTION ( 'NONE',  ( 0.7071067811865487940, 0.7071067811865463515, 0.000000000000000000 ) ) ;
#109945=AXIS2_PLACEMENT_3D ( 'NONE', #93296, #27305, #47000 ) ;
#109948=DIRECTION ( 'NONE',  ( 0.7071067811865486830, -0.7071067811865464625, -0.000000000000000000 ) ) ;
#109949=VECTOR ( 'NONE', #88310, 999.9999999999998863 ) ;
#109952=CARTESIAN_POINT ( 'NONE',  ( -2.816011393730999401, 28.73617430169785436, 5.000000000000000000 ) ) ;
#109953=CARTESIAN_POINT ( 'NONE',  ( 33.18398860626899705, 28.73617430169810305, 5.000000000000000000 ) ) ;
#109954=CARTESIAN_POINT ( 'NONE',  ( 19.49999999999986855, 21.43112307739196609, 4.000000000000000000 ) ) ;
#109955=CARTESIAN_POINT ( 'NONE',  ( -11.51078643762690490, -27.52281430457047406, 5.000000000000000000 ) ) ;
#109956=EDGE_CURVE ( 'NONE', #133790, #79052, #69069, .T. ) ;
#109959=AXIS2_PLACEMENT_3D ( 'NONE', #114625, #59577, #8679 ) ;
#109960=ORIENTED_EDGE ( 'NONE', *, *, #130779, .F. ) ;
#109961=ADVANCED_FACE ( 'NONE', ( #125594 ), #70532, .T. ) ;
#109963=ORIENTED_EDGE ( 'NONE', *, *, #26078, .T. ) ;
#109965=ORIENTED_EDGE ( 'NONE', *, *, #140217, .F. ) ;
#109966=ADVANCED_FACE ( 'NONE', ( #60341 ), #104525, .T. ) ;
#109967=DIRECTION ( 'NONE',  ( 0.6830127018922181881, 0.6830127018922202975, -0.2588190451025214056 ) ) ;
#109968=DIRECTION ( 'NONE',  ( -0.7071067811865486830, -0.7071067811865464625, 0.000000000000000000 ) ) ;
#109970=CARTESIAN_POINT ( 'NONE',  ( -8.994519915287490619, 28.92564299267944250, 4.000000000000000000 ) ) ;
#109971=VERTEX_POINT ( 'NONE', #102421 ) ;
#109974=CARTESIAN_POINT ( 'NONE',  ( 14.99999999999989164, -11.35517001088070721, -1.126524801160074363 ) ) ;
#109976=FACE_OUTER_BOUND ( 'NONE', #86781, .T. ) ;
#109977=AXIS2_PLACEMENT_3D ( 'NONE', #117947, #128856, #16511 ) ;
#109978=ADVANCED_FACE ( 'NONE', ( #80659 ), #61766, .F. ) ;
#109981=ORIENTED_EDGE ( 'NONE', *, *, #124157, .T. ) ;
#109982=ORIENTED_EDGE ( 'NONE', *, *, #61555, .T. ) ;
#109984=DIRECTION ( 'NONE',  ( -0.000000000000000000, 0.000000000000000000, 1.000000000000000000 ) ) ;
#109986=FACE_OUTER_BOUND ( 'NONE', #108056, .T. ) ;
#109988=DIRECTION ( 'NONE',  ( 0.7071067811865486830, -0.7071067811865464625, -0.000000000000000000 ) ) ;
#109989=DIRECTION ( 'NONE',  ( -0.000000000000000000, -0.000000000000000000, 1.000000000000000000 ) ) ;
#109991=CARTESIAN_POINT ( 'NONE',  ( 51.29974487139158867, -27.71228299555242103, 4.000000000000000000 ) ) ;
#109992=DIRECTION ( 'NONE',  ( -0.3543493200069162685, -0.000000000000000000, -0.9351131265310288487 ) ) ;
#109993=ORIENTED_EDGE ( 'NONE', *, *, #110587, .T. ) ;
#109994=CARTESIAN_POINT ( 'NONE',  ( -42.18398860626899705, 28.73617430169816700, 5.000000000000000000 ) ) ;
#109995=ORIENTED_EDGE ( 'NONE', *, *, #50229, .T. ) ;
#109996=CARTESIAN_POINT ( 'NONE',  ( 12.32816939922344268, 20.25929247661551713, 4.000000000000000000 ) ) ;
#109997=ORIENTED_EDGE ( 'NONE', *, *, #43720, .T. ) ;
#109998=DIRECTION ( 'NONE',  ( 0.7071067811865486830, -0.7071067811865464625, -0.000000000000000000 ) ) ;
#109999=FACE_OUTER_BOUND ( 'NONE', #48016, .T. ) ;
#110000=ORIENTED_EDGE ( 'NONE', *, *, #8101, .F. ) ;
#110001=CARTESIAN_POINT ( 'NONE',  ( 26.99999999999982236, 14.87792677143811737, -11.06722581663433935 ) ) ;
#110002=EDGE_CURVE ( 'NONE', #100802, #132053, #118966, .T. ) ;
#110003=ORIENTED_EDGE ( 'NONE', *, *, #27243, .T. ) ;
#110005=CARTESIAN_POINT ( 'NONE',  ( -5.999999999999952927, -19.06887692260761469, 4.000000000000000000 ) ) ;
#110006=ORIENTED_EDGE ( 'NONE', *, *, #61419, .T. ) ;
#110007=CARTESIAN_POINT ( 'NONE',  ( -42.48921356237308800, -27.52281430457085065, 5.000000000000000000 ) ) ;
#110008=EDGE_CURVE ( 'NONE', #142445, #62352, #141446, .T. ) ;
#110010=CARTESIAN_POINT ( 'NONE',  ( -5.186508646023577640, -15.74070752338412049, 8.904080028138954717 ) ) ;
#110011=FACE_OUTER_BOUND ( 'NONE', #57762, .T. ) ;
#110013=FACE_OUTER_BOUND ( 'NONE', #83596, .T. ) ;
#110014=LINE ( 'NONE', #97719, #52968 ) ;
#110017=DIRECTION ( 'NONE',  ( -0.7071067811865486830, 0.7071067811865464625, 0.000000000000000000 ) ) ;
#110018=DIRECTION ( 'NONE',  ( -0.7071067811865486830, -0.7071067811865464625, 0.000000000000000000 ) ) ;
#110019=ORIENTED_EDGE ( 'NONE', *, *, #17458, .T. ) ;
#110020=ORIENTED_EDGE ( 'NONE', *, *, #115643, .T. ) ;
#110021=EDGE_CURVE ( 'NONE', #1441, #127035, #27671, .T. ) ;
#110022=CARTESIAN_POINT ( 'NONE',  ( 1.998069433179001653, -22.22500000000000142, 4.500000000000000888 ) ) ;
#110024=CARTESIAN_POINT ( 'NONE',  ( 14.67183060077636902, -6.740707523384207533, 4.000000000000000000 ) ) ;
#110025=PLANE ( 'NONE',  #132650 ) ;
#110026=CARTESIAN_POINT ( 'NONE',  ( 78.18398860626899705, 28.73617430169841924, 5.000000000000000000 ) ) ;
#110027=EDGE_LOOP ( 'NONE', ( #50812, #126634, #59523, #73552 ) ) ;
#110028=LINE ( 'NONE', #54276, #137813 ) ;
#110029=CARTESIAN_POINT ( 'NONE',  ( -7.499999999999951150, -20.56887692260760048, 4.000000000000000000 ) ) ;
#110030=FACE_OUTER_BOUND ( 'NONE', #93734, .T. ) ;
#110032=DIRECTION ( 'NONE',  ( 2.781805975412905274E-17, -0.3543493200069152138, 0.9351131265310292928 ) ) ;
#110033=CARTESIAN_POINT ( 'NONE',  ( 0.000000000000000000, 0.000000000000000000, 5.000000000000000000 ) ) ;
#110036=DIRECTION ( 'NONE',  ( 0.7071067811865486830, -0.7071067811865464625, -0.000000000000000000 ) ) ;
#110039=DIRECTION ( 'NONE',  ( 0.7071067811865487940, -0.7071067811865463515, 0.000000000000000000 ) ) ;
#110040=PLANE ( 'NONE',  #114019 ) ;
#110041=ORIENTED_EDGE ( 'NONE', *, *, #3443, .F. ) ;
#110042=VECTOR ( 'NONE', #73687, 1000.000000000000000 ) ;
#110043=EDGE_LOOP ( 'NONE', ( #141960, #2376, #67656, #6205 ) ) ;
#110044=ORIENTED_EDGE ( 'NONE', *, *, #107788, .F. ) ;
#110051=DIRECTION ( 'NONE',  ( -0.000000000000000000, 0.000000000000000000, 1.000000000000000000 ) ) ;
#110054=ORIENTED_EDGE ( 'NONE', *, *, #33932, .T. ) ;
#110055=LINE ( 'NONE', #132583, #37350 ) ;
#110057=DIRECTION ( 'NONE',  ( -0.7071067811865487940, 0.7071067811865463515, 0.000000000000000000 ) ) ;
#110058=ORIENTED_EDGE ( 'NONE', *, *, #135777, .F. ) ;
#110061=CARTESIAN_POINT ( 'NONE',  ( -18.00548008471250583, 28.92564299267925776, 4.000000000000000000 ) ) ;
#110062=EDGE_CURVE ( 'NONE', #81231, #69434, #136368, .T. ) ;
#110063=EDGE_CURVE ( 'NONE', #115305, #49295, #61085, .T. ) ;
#110066=CARTESIAN_POINT ( 'NONE',  ( 0.000000000000000000, 0.000000000000000000, 5.000000000000000000 ) ) ;
#110067=DIRECTION ( 'NONE',  ( 0.7071067811865487940, -0.7071067811865463515, -0.000000000000000000 ) ) ;
#110069=DIRECTION ( 'NONE',  ( -0.6830127018922180770, -0.6830127018922204085, -0.2588190451025213501 ) ) ;
#110070=ADVANCED_FACE ( 'NONE', ( #40714 ), #127730, .F. ) ;
#110072=VECTOR ( 'NONE', #139860, 1000.000000000000000 ) ;
#110073=ADVANCED_FACE ( 'NONE', ( #129852 ), #5894, .F. ) ;
#110074=ORIENTED_EDGE ( 'NONE', *, *, #52644, .F. ) ;
#110075=VECTOR ( 'NONE', #83962, 1000.000000000000000 ) ;
#110076=VERTEX_POINT ( 'NONE', #72673 ) ;
#110077=CARTESIAN_POINT ( 'NONE',  ( 63.29974487139158867, -27.71228299555250274, 4.000000000000000000 ) ) ;
#110078=EDGE_CURVE ( 'NONE', #41370, #128174, #105930, .T. ) ;
#110079=VERTEX_POINT ( 'NONE', #74790 ) ;
#110080=ORIENTED_EDGE ( 'NONE', *, *, #31495, .T. ) ;
#110082=EDGE_CURVE ( 'NONE', #61139, #58008, #139338, .T. ) ;
#110083=ADVANCED_FACE ( 'NONE', ( #63898 ), #128441, .T. ) ;
#110084=CARTESIAN_POINT ( 'NONE',  ( 4.171830600776440079, 15.75929247661555976, 4.000000000000000000 ) ) ;
#110085=EDGE_LOOP ( 'NONE', ( #35594, #49386, #109364 ) ) ;
#110088=CARTESIAN_POINT ( 'NONE',  ( -21.18398860626899349, 28.73617430169802134, 5.000000000000000000 ) ) ;
#110089=DIRECTION ( 'NONE',  ( 0.7071067811865487940, 0.7071067811865463515, 0.000000000000000000 ) ) ;
#110090=EDGE_LOOP ( 'NONE', ( #113975, #60414, #100542, #136915, #117681 ) ) ;
#110091=EDGE_CURVE ( 'NONE', #14957, #58958, #94240, .T. ) ;
#110092=CARTESIAN_POINT ( 'NONE',  ( 15.48921356237309510, -27.52281430457066236, 5.000000000000000000 ) ) ;
#110093=ORIENTED_EDGE ( 'NONE', *, *, #78775, .F. ) ;
#110094=LINE ( 'NONE', #76806, #38786 ) ;
#110096=DIRECTION ( 'NONE',  ( -0.7071067811865487940, 0.7071067811865463515, -0.000000000000000000 ) ) ;
#110098=LINE ( 'NONE', #9329, #11109 ) ;
#110099=ORIENTED_EDGE ( 'NONE', *, *, #84415, .T. ) ;
#110100=ORIENTED_EDGE ( 'NONE', *, *, #7291, .F. ) ;
#110103=CARTESIAN_POINT ( 'NONE',  ( 27.48921356237309155, -27.52281430457074762, 5.000000000000000000 ) ) ;
#110104=CARTESIAN_POINT ( 'NONE',  ( -25.49999999999982236, 22.01701374228153085, 2.453858888625688905 ) ) ;
#110105=PLANE ( 'NONE',  #135271 ) ;
#110107=CARTESIAN_POINT ( 'NONE',  ( 60.48921356237309510, -27.52281430457097500, 5.000000000000000000 ) ) ;
#110108=DIRECTION ( 'NONE',  ( 0.7071067811865486830, -0.7071067811865464625, -0.000000000000000000 ) ) ;
#110109=FACE_OUTER_BOUND ( 'NONE', #43498, .T. ) ;
#110110=DIRECTION ( 'NONE',  ( -0.7071067811865486830, -0.7071067811865464625, 0.000000000000000000 ) ) ;
#110111=FACE_OUTER_BOUND ( 'NONE', #115049, .T. ) ;
#110112=ADVANCED_FACE ( 'NONE', ( #44296 ), #110920, .F. ) ;
#110113=DIRECTION ( 'NONE',  ( 0.6830127018922181881, 0.6830127018922202975, -0.2588190451025214056 ) ) ;
#110114=PLANE ( 'NONE',  #33301 ) ;
#110115=ORIENTED_EDGE ( 'NONE', *, *, #57360, .F. ) ;
#110116=EDGE_CURVE ( 'NONE', #68584, #142173, #88509, .T. ) ;
#110117=ORIENTED_EDGE ( 'NONE', *, *, #75617, .F. ) ;
#110122=EDGE_CURVE ( 'NONE', #115190, #97236, #119654, .T. ) ;
#110123=EDGE_LOOP ( 'NONE', ( #42648, #100161, #138880, #27871 ) ) ;
#110124=LINE ( 'NONE', #22388, #19015 ) ;
#110126=CARTESIAN_POINT ( 'NONE',  ( 25.49999999999982236, 5.696342897626525570, -7.587980461218338135 ) ) ;
#110127=CARTESIAN_POINT ( 'NONE',  ( -27.32816939922334143, -18.74070752338409562, 4.000000000000000000 ) ) ;
#110128=VERTEX_POINT ( 'NONE', #75483 ) ;
#110131=FACE_OUTER_BOUND ( 'NONE', #76122, .T. ) ;
#110132=AXIS2_PLACEMENT_3D ( 'NONE', #59227, #127286, #27984 ) ;
#110134=VERTEX_POINT ( 'NONE', #130589 ) ;
#110137=VECTOR ( 'NONE', #77818, 1000.000000000000000 ) ;
#110138=LINE ( 'NONE', #130508, #136970 ) ;
#110139=EDGE_CURVE ( 'NONE', #70259, #136354, #55159, .T. ) ;
#110141=ORIENTED_EDGE ( 'NONE', *, *, #110917, .T. ) ;
#110142=VERTEX_POINT ( 'NONE', #33437 ) ;
#110143=ORIENTED_EDGE ( 'NONE', *, *, #86758, .T. ) ;
#110145=DIRECTION ( 'NONE',  ( 1.000000000000000000, 0.000000000000000000, 0.000000000000000000 ) ) ;
#110146=PLANE ( 'NONE',  #134477 ) ;
#110147=FACE_OUTER_BOUND ( 'NONE', #6650, .T. ) ;
#110148=LINE ( 'NONE', #111598, #14863 ) ;
#110149=ORIENTED_EDGE ( 'NONE', *, *, #36289, .T. ) ;
#110150=CARTESIAN_POINT ( 'NONE',  ( -18.18398860626898994, 28.73617430169800002, 5.000000000000000000 ) ) ;
#110151=EDGE_CURVE ( 'NONE', #70446, #32019, #98643, .T. ) ;
#110152=AXIS2_PLACEMENT_3D ( 'NONE', #38713, #105378, #116270 ) ;
#110154=CARTESIAN_POINT ( 'NONE',  ( 38.99451991528749062, 28.92564299267965211, 4.000000000000000000 ) ) ;
#110155=VERTEX_POINT ( 'NONE', #142179 ) ;
#110156=CARTESIAN_POINT ( 'NONE',  ( -34.57058949319514340, 22.20469455417149618, 4.123089426795147006 ) ) ;
#110157=DIRECTION ( 'NONE',  ( 0.7071067811865487940, -0.7071067811865463515, 0.000000000000000000 ) ) ;
#110158=ORIENTED_EDGE ( 'NONE', *, *, #129858, .F. ) ;
#110159=DIRECTION ( 'NONE',  ( -0.6830127018922181881, 0.6830127018922202975, -0.2588190451025214056 ) ) ;
#110160=ORIENTED_EDGE ( 'NONE', *, *, #76, .F. ) ;
#110161=ADVANCED_FACE ( 'NONE', ( #56630 ), #89216, .F. ) ;
#110162=ORIENTED_EDGE ( 'NONE', *, *, #93949, .T. ) ;
#110163=EDGE_CURVE ( 'NONE', #63317, #91527, #21078, .T. ) ;
#110164=CARTESIAN_POINT ( 'NONE',  ( 1.499999999999987566, 8.319652575858389909, -8.582050562765823898 ) ) ;
#110165=LINE ( 'NONE', #99280, #97001 ) ;
#110166=ORIENTED_EDGE ( 'NONE', *, *, #121642, .F. ) ;
#110167=LINE ( 'NONE', #44243, #111385 ) ;
#110169=PLANE ( 'NONE',  #80003 ) ;
#110170=VECTOR ( 'NONE', #13938, 1000.000000000000000 ) ;
#110172=VECTOR ( 'NONE', #76113, 1000.000000000000000 ) ;
#110173=DIRECTION ( 'NONE',  ( -0.6830127018922180770, -0.6830127018922204085, -0.2588190451025213501 ) ) ;
#110174=LINE ( 'NONE', #2099, #37358 ) ;
#110176=LINE ( 'NONE', #102192, #39877 ) ;
#110177=FACE_OUTER_BOUND ( 'NONE', #33264, .T. ) ;
#110178=DIRECTION ( 'NONE',  ( 0.6830127018922180770, -0.6830127018922204085, -0.2588190451025213501 ) ) ;
#110179=CARTESIAN_POINT ( 'NONE',  ( 39.18398860626899705, 28.73617430169814568, 5.000000000000000000 ) ) ;
#110181=LINE ( 'NONE', #10854, #87640 ) ;
#110182=AXIS2_PLACEMENT_3D ( 'NONE', #60130, #79774, #123955 ) ;
#110183=LINE ( 'NONE', #134112, #134539 ) ;
#110184=CARTESIAN_POINT ( 'NONE',  ( -26.57672154193630476, 11.25929247661559529, 17.85071094206590203 ) ) ;
#110185=ORIENTED_EDGE ( 'NONE', *, *, #92167, .F. ) ;
#110189=EDGE_CURVE ( 'NONE', #131796, #123357, #97942, .T. ) ;
#110190=ORIENTED_EDGE ( 'NONE', *, *, #37133, .F. ) ;
#110191=ORIENTED_EDGE ( 'NONE', *, *, #34636, .T. ) ;
#110192=ORIENTED_EDGE ( 'NONE', *, *, #1169, .T. ) ;
#110193=LINE ( 'NONE', #2866, #38738 ) ;
#110194=CARTESIAN_POINT ( 'NONE',  ( 12.32816939922343913, -12.74070752338415957, 4.000000000000000000 ) ) ;
#110195=ORIENTED_EDGE ( 'NONE', *, *, #73311, .T. ) ;
#110198=DIRECTION ( 'NONE',  ( -0.7071067811865486830, -0.7071067811865464625, 0.000000000000000000 ) ) ;
#110199=LINE ( 'NONE', #110902, #83679 ) ;
#110200=ORIENTED_EDGE ( 'NONE', *, *, #53483, .F. ) ;
#110202=FACE_OUTER_BOUND ( 'NONE', #72229, .T. ) ;
#110203=DIRECTION ( 'NONE',  ( 0.6830127018922180770, 0.6830127018922202975, -0.2588190451025213501 ) ) ;
#110204=CARTESIAN_POINT ( 'NONE',  ( 24.20969143188526118, 6.176090689687629975, 5.000000000000000000 ) ) ;
#110205=LINE ( 'NONE', #131268, #74660 ) ;
#110208=CARTESIAN_POINT ( 'NONE',  ( 6.489213562373093325, -27.52281430457059841, 5.000000000000000000 ) ) ;
#110209=ORIENTED_EDGE ( 'NONE', *, *, #136897, .T. ) ;
#110210=VERTEX_POINT ( 'NONE', #142870 ) ;
#110212=ORIENTED_EDGE ( 'NONE', *, *, #94565, .F. ) ;
#110213=CARTESIAN_POINT ( 'NONE',  ( 26.99451991528749417, 28.92564299267956685, 4.000000000000000000 ) ) ;
#110214=DIRECTION ( 'NONE',  ( 0.7071067811865486830, -0.7071067811865464625, -0.000000000000000000 ) ) ;
#110215=AXIS2_PLACEMENT_3D ( 'NONE', #112200, #71548, #91174 ) ;
#110216=DIRECTION ( 'NONE',  ( -0.7071067811865486830, -0.7071067811865463515, 0.000000000000000000 ) ) ;
#110217=LINE ( 'NONE', #98645, #60582 ) ;
#110218=LINE ( 'NONE', #77641, #60418 ) ;
#110220=VERTEX_POINT ( 'NONE', #86365 ) ;
#110221=ORIENTED_EDGE ( 'NONE', *, *, #110862, .T. ) ;
#110222=CARTESIAN_POINT ( 'NONE',  ( 4.499999999999968914, -8.568876922607726598, 4.000000000000000000 ) ) ;
#110223=VERTEX_POINT ( 'NONE', #66747 ) ;
#110224=ORIENTED_EDGE ( 'NONE', *, *, #60751, .F. ) ;
#110226=ORIENTED_EDGE ( 'NONE', *, *, #10728, .T. ) ;
#110227=PLANE ( 'NONE',  #123211 ) ;
#110229=LINE ( 'NONE', #65361, #126520 ) ;
#110230=PLANE ( 'NONE',  #15941 ) ;
#110231=AXIS2_PLACEMENT_3D ( 'NONE', #85146, #52518, #96703 ) ;
#110232=ADVANCED_FACE ( 'NONE', ( #67483 ), #9463, .F. ) ;
#110234=EDGE_CURVE ( 'NONE', #143094, #94959, #132009, .T. ) ;
#110235=EDGE_LOOP ( 'NONE', ( #66208, #12316, #40870, #127809 ) ) ;
#110236=DIRECTION ( 'NONE',  ( -0.000000000000000000, -0.3543493200069152693, 0.9351131265310292928 ) ) ;
#110237=ADVANCED_FACE ( 'NONE', ( #76934 ), #121107, .F. ) ;
#110238=ORIENTED_EDGE ( 'NONE', *, *, #122185, .T. ) ;
#110239=ORIENTED_EDGE ( 'NONE', *, *, #41024, .F. ) ;
#110240=EDGE_LOOP ( 'NONE', ( #46179, #130393, #87200, #31775 ) ) ;
#110242=CARTESIAN_POINT ( 'NONE',  ( 11.99451991528749417, 28.92564299267946382, 4.000000000000000000 ) ) ;
#110244=LINE ( 'NONE', #86403, #59889 ) ;
#110246=ADVANCED_FACE ( 'NONE', ( #60162 ), #123988, .F. ) ;
#110247=DIRECTION ( 'NONE',  ( -0.6830127018922180770, -0.6830127018922204085, -0.2588190451025213501 ) ) ;
#110249=DIRECTION ( 'NONE',  ( -0.7071067811865487940, 0.7071067811865463515, -0.000000000000000000 ) ) ;
#110250=ADVANCED_FACE ( 'NONE', ( #57321 ), #136266, .F. ) ;
#110251=AXIS2_PLACEMENT_3D ( 'NONE', #128960, #117345, #139869 ) ;
#110252=FACE_BOUND ( 'NONE', #88241, .T. ) ;
#110253=EDGE_LOOP ( 'NONE', ( #122956, #100989, #67443, #52693 ) ) ;
#110254=EDGE_CURVE ( 'NONE', #133807, #31371, #4258, .T. ) ;
#110256=LINE ( 'NONE', #66786, #32884 ) ;
#110257=PLANE ( 'NONE',  #99503 ) ;
#110258=EDGE_LOOP ( 'NONE', ( #97199, #91189, #32106, #4403 ) ) ;
#110259=CARTESIAN_POINT ( 'NONE',  ( -20.81601139373100295, 28.73617430169773002, 5.000000000000000000 ) ) ;
#110260=ORIENTED_EDGE ( 'NONE', *, *, #921, .F. ) ;
#110261=VERTEX_POINT ( 'NONE', #45733 ) ;
#110262=CARTESIAN_POINT ( 'NONE',  ( 13.49999999999990408, 19.39370406404968250, 1.459788787078170502 ) ) ;
#110263=EDGE_CURVE ( 'NONE', #96071, #94260, #37699, .T. ) ;
#110265=ORIENTED_EDGE ( 'NONE', *, *, #4991, .T. ) ;
#110266=VECTOR ( 'NONE', #77821, 1000.000000000000114 ) ;
#110267=VECTOR ( 'NONE', #129865, 999.9999999999998863 ) ;
#110269=VERTEX_POINT ( 'NONE', #134149 ) ;
#110270=LINE ( 'NONE', #19709, #83519 ) ;
#110271=FACE_OUTER_BOUND ( 'NONE', #53489, .T. ) ;
#110272=DIRECTION ( 'NONE',  ( 0.7071067811865486830, -0.7071067811865464625, -0.000000000000000000 ) ) ;
#110273=ORIENTED_EDGE ( 'NONE', *, *, #115950, .F. ) ;
#110274=CARTESIAN_POINT ( 'NONE',  ( -21.18398860626899349, 28.73617430169802134, 5.000000000000000000 ) ) ;
#110275=LINE ( 'NONE', #55215, #94471 ) ;
#110276=VECTOR ( 'NONE', #90606, 999.9999999999998863 ) ;
#110278=PLANE ( 'NONE',  #136581 ) ;
#110279=CYLINDRICAL_SURFACE ( 'NONE', #136252, 0.5000000000000004441 ) ;
#110280=DIRECTION ( 'NONE',  ( -0.7071067811865486830, 0.7071067811865464625, 0.000000000000000000 ) ) ;
#110281=FACE_OUTER_BOUND ( 'NONE', #42675, .T. ) ;
#110282=VERTEX_POINT ( 'NONE', #79082 ) ;
#110283=EDGE_CURVE ( 'NONE', #120806, #118332, #36262, .T. ) ;
#110284=ORIENTED_EDGE ( 'NONE', *, *, #72994, .T. ) ;
#110285=ORIENTED_EDGE ( 'NONE', *, *, #104943, .F. ) ;
#110286=CARTESIAN_POINT ( 'NONE',  ( -42.18398860626899705, 28.73617430169816700, 5.000000000000000000 ) ) ;
#110287=PLANE ( 'NONE',  #5068 ) ;
#110288=ORIENTED_EDGE ( 'NONE', *, *, #12717, .T. ) ;
#110289=ORIENTED_EDGE ( 'NONE', *, *, #3651, .T. ) ;
#110291=DIRECTION ( 'NONE',  ( -0.6830127018922181881, 0.6830127018922202975, -0.2588190451025214056 ) ) ;
#110292=CARTESIAN_POINT ( 'NONE',  ( 47.99451991528749062, 28.92564299267971251, 4.000000000000000000 ) ) ;
#110293=ORIENTED_EDGE ( 'NONE', *, *, #110082, .T. ) ;
#110294=DIRECTION ( 'NONE',  ( 0.6830127018922181881, 0.6830127018922202975, -0.2588190451025214056 ) ) ;
#110295=EDGE_CURVE ( 'NONE', #142173, #123033, #92750, .T. ) ;
#110296=DIRECTION ( 'NONE',  ( -0.3543493200069162685, -0.000000000000000000, -0.9351131265310288487 ) ) ;
#110299=CARTESIAN_POINT ( 'NONE',  ( -30.18398860626900060, 28.73617430169808173, 5.000000000000000000 ) ) ;
#110300=ORIENTED_EDGE ( 'NONE', *, *, #28044, .T. ) ;
#110302=CARTESIAN_POINT ( 'NONE',  ( -77.99451991528749772, 28.92564299267992567, 4.000000000000000000 ) ) ;
#110304=DIRECTION ( 'NONE',  ( 0.7071067811865486830, -0.7071067811865464625, -0.000000000000000000 ) ) ;
#110305=DIRECTION ( 'NONE',  ( -0.3543493200069163240, 0.000000000000000000, -0.9351131265310288487 ) ) ;
#110306=EDGE_LOOP ( 'NONE', ( #142399, #92526, #74898, #93673 ) ) ;
#110307=VECTOR ( 'NONE', #122529, 1000.000000000000000 ) ;
#110309=EDGE_LOOP ( 'NONE', ( #87267, #38266, #36651, #39006 ) ) ;
#110310=PLANE ( 'NONE',  #100687 ) ;
#110311=PLANE ( 'NONE',  #120998 ) ;
#110312=DIRECTION ( 'NONE',  ( 0.7071067811865487940, 0.7071067811865463515, 0.000000000000000000 ) ) ;
#110313=VERTEX_POINT ( 'NONE', #125409 ) ;
#110314=EDGE_CURVE ( 'NONE', #49875, #140112, #13046, .T. ) ;
#110315=CARTESIAN_POINT ( 'NONE',  ( -19.05000000000000071, 3.174999999999997158, 4.000000000000000000 ) ) ;
#110316=CARTESIAN_POINT ( 'NONE',  ( -34.92500000000001137, 21.72500000000000142, 5.000000000000000000 ) ) ;
#110317=VECTOR ( 'NONE', #127121, 1000.000000000000000 ) ;
#110318=VERTEX_POINT ( 'NONE', #2149 ) ;
#110320=LINE ( 'NONE', #131397, #109412 ) ;
#110322=CARTESIAN_POINT ( 'NONE',  ( 27.18398860626900060, 28.73617430169806042, 5.000000000000000000 ) ) ;
#110323=VECTOR ( 'NONE', #16661, 1000.000000000000000 ) ;
#110324=DIRECTION ( 'NONE',  ( -0.000000000000000000, 0.000000000000000000, 1.000000000000000000 ) ) ;
#110326=EDGE_CURVE ( 'NONE', #69443, #53276, #26797, .T. ) ;
#110327=ORIENTED_EDGE ( 'NONE', *, *, #94380, .T. ) ;
#110328=CARTESIAN_POINT ( 'NONE',  ( -13.10332671766740020, 3.690788593506699300, 4.000000000000000000 ) ) ;
#110329=DIRECTION ( 'NONE',  ( -0.000000000000000000, -0.3543493200069152693, 0.9351131265310292928 ) ) ;
#110331=VECTOR ( 'NONE', #19714, 1000.000000000000000 ) ;
#110333=DIRECTION ( 'NONE',  ( 0.6830127018922181881, 0.6830127018922202975, -0.2588190451025214056 ) ) ;
#110334=DIRECTION ( 'NONE',  ( -0.000000000000000000, -0.000000000000000000, 1.000000000000000000 ) ) ;
#110335=AXIS2_PLACEMENT_3D ( 'NONE', #103995, #138820, #28636 ) ;
#110336=ORIENTED_EDGE ( 'NONE', *, *, #11969, .T. ) ;
#110338=DIRECTION ( 'NONE',  ( 0.7071067811865487940, -0.7071067811865463515, 0.000000000000000000 ) ) ;
#110339=DIRECTION ( 'NONE',  ( 1.000000000000000000, 0.000000000000000000, 0.000000000000000000 ) ) ;
#110340=VECTOR ( 'NONE', #140178, 1000.000000000000000 ) ;
#110341=DIRECTION ( 'NONE',  ( -0.6830127018922181881, 0.6830127018922202975, -0.2588190451025214056 ) ) ;
#110342=LINE ( 'NONE', #22607, #101522 ) ;
#110344=CARTESIAN_POINT ( 'NONE',  ( 8.148183550381396856, 17.25929247661554911, 8.802941693769220421 ) ) ;
#110345=ORIENTED_EDGE ( 'NONE', *, *, #115035, .T. ) ;
#110346=VERTEX_POINT ( 'NONE', #70355 ) ;
#110347=PLANE ( 'NONE',  #106775 ) ;
#110348=EDGE_CURVE ( 'NONE', #61052, #32802, #80490, .T. ) ;
#110349=ORIENTED_EDGE ( 'NONE', *, *, #59592, .F. ) ;
#110350=VECTOR ( 'NONE', #74465, 1000.000000000000114 ) ;
#110352=LINE ( 'NONE', #121244, #73416 ) ;
#110353=DIRECTION ( 'NONE',  ( -0.7071067811865487940, 0.7071067811865463515, -0.000000000000000000 ) ) ;
#110354=EDGE_LOOP ( 'NONE', ( #95620, #19371, #85914, #59979 ) ) ;
#110355=PLANE ( 'NONE',  #23036 ) ;
#110356=DIRECTION ( 'NONE',  ( 0.6830127018922180770, -0.6830127018922204085, -0.2588190451025213501 ) ) ;
#110357=CARTESIAN_POINT ( 'NONE',  ( 2.293207492759234523, 20.25929247661550647, 20.83292124670813905 ) ) ;
#110358=AXIS2_PLACEMENT_3D ( 'NONE', #86005, #88159, #142544 ) ;
#110361=ORIENTED_EDGE ( 'NONE', *, *, #81379, .T. ) ;
#110362=EDGE_CURVE ( 'NONE', #36893, #109568, #41230, .T. ) ;
#110363=PLANE ( 'NONE',  #14037 ) ;
#110365=CARTESIAN_POINT ( 'NONE',  ( -14.51078643762690490, -27.52281430457045275, 5.000000000000000000 ) ) ;
#110366=LINE ( 'NONE', #66897, #8001 ) ;
#110368=CARTESIAN_POINT ( 'NONE',  ( 42.48921356237308800, -27.52281430457085065, 5.000000000000000000 ) ) ;
#110369=FACE_OUTER_BOUND ( 'NONE', #52384, .T. ) ;
#110371=AXIS2_PLACEMENT_3D ( 'NONE', #7363, #62499, #106673 ) ;
#110373=FACE_OUTER_BOUND ( 'NONE', #64415, .T. ) ;
#110374=AXIS2_PLACEMENT_3D ( 'NONE', #128935, #139850, #6389 ) ;
#110375=DIRECTION ( 'NONE',  ( -0.7071067811865486830, -0.7071067811865464625, 0.000000000000000000 ) ) ;
#110376=ORIENTED_EDGE ( 'NONE', *, *, #24690, .F. ) ;
#110377=ORIENTED_EDGE ( 'NONE', *, *, #48253, .T. ) ;
#110379=CARTESIAN_POINT ( 'NONE',  ( 34.49999999999975842, -10.04351517176474751, -1.623559851933744191 ) ) ;
#110380=VECTOR ( 'NONE', #6401, 1000.000000000000114 ) ;
#110381=VECTOR ( 'NONE', #16987, 1000.000000000000000 ) ;
#110382=DIRECTION ( 'NONE',  ( -0.7071067811865487940, 0.7071067811865463515, -0.000000000000000000 ) ) ;
#110383=ORIENTED_EDGE ( 'NONE', *, *, #75422, .F. ) ;
#110385=EDGE_CURVE ( 'NONE', #1646, #111099, #84070, .T. ) ;
#110386=DIRECTION ( 'NONE',  ( -0.3543493200069162685, -0.000000000000000000, -0.9351131265310288487 ) ) ;
#110388=ORIENTED_EDGE ( 'NONE', *, *, #77637, .F. ) ;
#110390=VERTEX_POINT ( 'NONE', #49299 ) ;
#110391=VERTEX_POINT ( 'NONE', #107203 ) ;
#110392=DIRECTION ( 'NONE',  ( 0.7071067811865486830, -0.7071067811865464625, -0.000000000000000000 ) ) ;
#110394=DIRECTION ( 'NONE',  ( 0.3543493200069162685, -0.000000000000000000, -0.9351131265310288487 ) ) ;
#110395=DIRECTION ( 'NONE',  ( 1.000000000000000000, -0.000000000000000000, 0.000000000000000000 ) ) ;
#110396=VERTEX_POINT ( 'NONE', #129664 ) ;
#110397=LINE ( 'NONE', #51780, #99733 ) ;
#110399=EDGE_LOOP ( 'NONE', ( #63674, #135639, #52261, #117161, #75746 ) ) ;
#110402=CARTESIAN_POINT ( 'NONE',  ( -66.48921356237309510, -27.52281430457101763, 5.000000000000000000 ) ) ;
#110404=DIRECTION ( 'NONE',  ( 0.6830127018922181881, 0.6830127018922202975, -0.2588190451025214056 ) ) ;
#110405=FACE_OUTER_BOUND ( 'NONE', #79732, .T. ) ;
#110406=EDGE_CURVE ( 'NONE', #121985, #93231, #52115, .T. ) ;
#110407=ORIENTED_EDGE ( 'NONE', *, *, #83795, .F. ) ;
#110408=AXIS2_PLACEMENT_3D ( 'NONE', #100363, #68475, #36524 ) ;
#110409=DIRECTION ( 'NONE',  ( -0.7071067811865486830, -0.7071067811865464625, 0.000000000000000000 ) ) ;
#110411=EDGE_CURVE ( 'NONE', #78193, #140787, #16618, .T. ) ;
#110412=DIRECTION ( 'NONE',  ( -0.3543493200069162685, -0.000000000000000000, -0.9351131265310288487 ) ) ;
#110413=LINE ( 'NONE', #66240, #33944 ) ;
#110414=ORIENTED_EDGE ( 'NONE', *, *, #133552, .F. ) ;
#110415=EDGE_LOOP ( 'NONE', ( #54834, #81030, #20809, #128638 ) ) ;
#110416=LINE ( 'NONE', #141657, #137124 ) ;
#110417=ORIENTED_EDGE ( 'NONE', *, *, #43165, .T. ) ;
#110418=EDGE_CURVE ( 'NONE', #43072, #125864, #19484, .T. ) ;
#110419=EDGE_CURVE ( 'NONE', #35082, #68842, #128265, .T. ) ;
#110420=DIRECTION ( 'NONE',  ( -0.3543493200069162685, -0.000000000000000000, -0.9351131265310288487 ) ) ;
#110421=VERTEX_POINT ( 'NONE', #28231 ) ;
#110423=CARTESIAN_POINT ( 'NONE',  ( 10.49999999999992895, 0.4311230773921849169, 4.000000000000000000 ) ) ;
#110424=VECTOR ( 'NONE', #119107, 1000.000000000000000 ) ;
#110425=CARTESIAN_POINT ( 'NONE',  ( 0.000000000000000000, 0.000000000000000000, 5.000000000000000000 ) ) ;
#110426=DIRECTION ( 'NONE',  ( 0.7071067811865486830, -0.7071067811865464625, -0.000000000000000000 ) ) ;
#110427=EDGE_CURVE ( 'NONE', #33991, #99416, #116654, .T. ) ;
#110428=FACE_BOUND ( 'NONE', #26385, .T. ) ;
#110429=EDGE_CURVE ( 'NONE', #58244, #101765, #4995, .T. ) ;
#110430=DIRECTION ( 'NONE',  ( 0.6830127018922180770, -0.6830127018922202975, -0.2588190451025213501 ) ) ;
#110432=CARTESIAN_POINT ( 'NONE',  ( 32.67183060077624646, 14.25929247661557397, 4.000000000000000000 ) ) ;
#110433=DIRECTION ( 'NONE',  ( 1.000000000000000000, 0.000000000000000000, 0.000000000000000000 ) ) ;
#110434=CARTESIAN_POINT ( 'NONE',  ( -6.330102185472606280, 17.25929247661554555, 19.83885114516072790 ) ) ;
#110435=ORIENTED_EDGE ( 'NONE', *, *, #104754, .T. ) ;
#110436=DIRECTION ( 'NONE',  ( -0.7071067811865486830, -0.7071067811865464625, 0.000000000000000000 ) ) ;
#110437=EDGE_CURVE ( 'NONE', #42984, #29429, #6410, .T. ) ;
#110438=EDGE_LOOP ( 'NONE', ( #58849, #94436, #22377, #116007 ) ) ;
#110441=VERTEX_POINT ( 'NONE', #93486 ) ;
#110442=DIRECTION ( 'NONE',  ( -0.6830127018922180770, -0.6830127018922204085, -0.2588190451025213501 ) ) ;
#110443=VERTEX_POINT ( 'NONE', #96297 ) ;
#110444=DIRECTION ( 'NONE',  ( -0.7071067811865486830, -0.7071067811865464625, -0.000000000000000000 ) ) ;
#110445=EDGE_CURVE ( 'NONE', #32743, #88536, #38395, .T. ) ;
#110447=CARTESIAN_POINT ( 'NONE',  ( -34.17183060077623225, 21.75929247661550292, 4.000000000000000000 ) ) ;
#110448=DIRECTION ( 'NONE',  ( -0.7071067811865486830, 0.7071067811865464625, 0.000000000000000000 ) ) ;
#110449=FACE_OUTER_BOUND ( 'NONE', #119226, .T. ) ;
#110450=DIRECTION ( 'NONE',  ( 0.6830127018922180770, -0.6830127018922204085, -0.2588190451025213501 ) ) ;
#110451=CARTESIAN_POINT ( 'NONE',  ( 20.99999999999985434, -6.412538124160692909, 4.000000000000000000 ) ) ;
#110452=DIRECTION ( 'NONE',  ( -0.7071067811865486830, -0.7071067811865464625, 0.000000000000000000 ) ) ;
#110453=VERTEX_POINT ( 'NONE', #39105 ) ;
#110456=VERTEX_POINT ( 'NONE', #18017 ) ;
#110457=CARTESIAN_POINT ( 'NONE',  ( 0.000000000000000000, 0.000000000000000000, 5.000000000000000000 ) ) ;
#110459=ORIENTED_EDGE ( 'NONE', *, *, #62026, .T. ) ;
#110460=VECTOR ( 'NONE', #132594, 999.9999999999998863 ) ;
#110461=ORIENTED_EDGE ( 'NONE', *, *, #120572, .T. ) ;
#110463=VERTEX_POINT ( 'NONE', #51419 ) ;
#110464=DIRECTION ( 'NONE',  ( -0.7071067811865486830, -0.7071067811865464625, 0.000000000000000000 ) ) ;
#110465=VECTOR ( 'NONE', #8246, 1000.000000000000000 ) ;
#110466=VECTOR ( 'NONE', #86212, 1000.000000000000000 ) ;
#110467=ADVANCED_FACE ( 'NONE', ( #27487 ), #50694, .F. ) ;
#110468=CARTESIAN_POINT ( 'NONE',  ( 11.52487387214947212, 14.25929247661557575, 9.797011795316663552 ) ) ;
#110469=VECTOR ( 'NONE', #73353, 1000.000000000000000 ) ;
#110472=VERTEX_POINT ( 'NONE', #40544 ) ;
#110473=PLANE ( 'NONE',  #38819 ) ;
#110476=VECTOR ( 'NONE', #130240, 1000.000000000000000 ) ;
#110477=FACE_OUTER_BOUND ( 'NONE', #137425, .T. ) ;
#110478=PLANE ( 'NONE',  #63340 ) ;
#110480=ORIENTED_EDGE ( 'NONE', *, *, #57566, .T. ) ;
#110482=CARTESIAN_POINT ( 'NONE',  ( 13.49999999999990763, 6.431123077392117082, 4.000000000000000000 ) ) ;
#110483=PLANE ( 'NONE',  #37879 ) ;
#110484=VERTEX_POINT ( 'NONE', #137720 ) ;
#110485=FACE_OUTER_BOUND ( 'NONE', #10293, .T. ) ;
#110486=VERTEX_POINT ( 'NONE', #139145 ) ;
#110488=DIRECTION ( 'NONE',  ( -0.3543493200069163240, 0.000000000000000000, 0.9351131265310288487 ) ) ;
#110489=DIRECTION ( 'NONE',  ( -0.7071067811865486830, -0.7071067811865464625, 0.000000000000000000 ) ) ;
#110493=LINE ( 'NONE', #64896, #137417 ) ;
#110494=CARTESIAN_POINT ( 'NONE',  ( 7.499999999999954703, -2.173586137069128732, -4.605770156576094898 ) ) ;
#110495=VERTEX_POINT ( 'NONE', #54993 ) ;
#110496=EDGE_CURVE ( 'NONE', #132460, #41454, #20175, .T. ) ;
#110497=CARTESIAN_POINT ( 'NONE',  ( -23.51078643762690490, -27.52281430457038880, 5.000000000000000000 ) ) ;
#110498=ORIENTED_EDGE ( 'NONE', *, *, #51399, .T. ) ;
#110499=AXIS2_PLACEMENT_3D ( 'NONE', #111347, #109929, #10597 ) ;
#110503=VECTOR ( 'NONE', #59392, 1000.000000000000000 ) ;
#110505=DIRECTION ( 'NONE',  ( 1.000000000000000000, 0.000000000000000000, 0.000000000000000000 ) ) ;
#110506=CARTESIAN_POINT ( 'NONE',  ( -35.38161509397982485, -2.240707523384264377, 13.37739548510247189 ) ) ;
#110507=DIRECTION ( 'NONE',  ( 0.7071067811865486830, -0.7071067811865464625, -0.000000000000000000 ) ) ;
#110508=ORIENTED_EDGE ( 'NONE', *, *, #85138, .T. ) ;
#110509=LINE ( 'NONE', #77926, #108931 ) ;
#110514=DIRECTION ( 'NONE',  ( -0.6830127018922180770, -0.6830127018922204085, -0.2588190451025213501 ) ) ;
#110516=( BOUNDED_CURVE ( )  B_SPLINE_CURVE ( 3, ( #90717, #12407, #100854, #45793 ),
 .UNSPECIFIED., .F., .F. ) 
 B_SPLINE_CURVE_WITH_KNOTS ( ( 4, 4 ),
 ( 2.001653308786158991, 3.503810798801450854 ),
 .UNSPECIFIED. ) 
 CURVE ( )  GEOMETRIC_REPRESENTATION_ITEM ( )  RATIONAL_B_SPLINE_CURVE ( ( 1.000000000000000000, 0.8206354192515217250, 0.8206354192515217250, 1.000000000000000000 ) ) 
 REPRESENTATION_ITEM ( '' )  );
#110517=CARTESIAN_POINT ( 'NONE',  ( 15.18398860626900237, 28.73617430169797871, 5.000000000000000000 ) ) ;
#110518=CARTESIAN_POINT ( 'NONE',  ( 51.18398860626899705, 28.73617430169823095, 5.000000000000000000 ) ) ;
#110519=CARTESIAN_POINT ( 'NONE',  ( -8.999999999999934275, -0.03360074219773377668, 5.000000000000000000 ) ) ;
#110520=LINE ( 'NONE', #89509, #53435 ) ;
#110523=CARTESIAN_POINT ( 'NONE',  ( 18.32816939922340183, -9.740707523384180888, 4.000000000000000000 ) ) ;
#110524=VECTOR ( 'NONE', #129820, 1000.000000000000000 ) ;
#110527=DIRECTION ( 'NONE',  ( -0.7071067811865486830, -0.7071067811865464625, 0.000000000000000000 ) ) ;
#110528=LINE ( 'NONE', #11941, #71612 ) ;
#110530=ADVANCED_FACE ( 'NONE', ( #98476 ), #64417, .F. ) ;
#110531=LINE ( 'NONE', #33743, #46446 ) ;
#110532=LINE ( 'NONE', #134469, #47721 ) ;
#110533=ORIENTED_EDGE ( 'NONE', *, *, #22940, .F. ) ;
#110534=ADVANCED_FACE ( 'NONE', ( #130411 ), #108596, .F. ) ;
#110535=ORIENTED_EDGE ( 'NONE', *, *, #71162, .F. ) ;
#110537=CARTESIAN_POINT ( 'NONE',  ( 34.92499999999998295, -17.24070752338409562, 4.255531930566155197 ) ) ;
#110538=DIRECTION ( 'NONE',  ( -0.7071067811865486830, -0.7071067811865464625, 0.000000000000000000 ) ) ;
#110539=CYLINDRICAL_SURFACE ( 'NONE', #17920, 0.5000000000000004441 ) ;
#110542=CARTESIAN_POINT ( 'NONE',  ( 20.81601139373100295, 28.73617430169773002, 5.000000000000000000 ) ) ;
#110544=AXIS2_PLACEMENT_3D ( 'NONE', #94932, #118096, #63073 ) ;
#110546=EDGE_CURVE ( 'NONE', #137862, #104351, #32520, .T. ) ;
#110547=CARTESIAN_POINT ( 'NONE',  ( -27.72281430457040940, -21.72500000000000142, 5.000000000000000000 ) ) ;
#110549=CARTESIAN_POINT ( 'NONE',  ( -54.48921356237310221, -27.52281430457093236, 5.000000000000000000 ) ) ;
#110550=ORIENTED_EDGE ( 'NONE', *, *, #124422, .T. ) ;
#110551=EDGE_CURVE ( 'NONE', #129451, #96735, #97002, .T. ) ;
#110553=ORIENTED_EDGE ( 'NONE', *, *, #37793, .T. ) ;
#110554=DIRECTION ( 'NONE',  ( -0.3543493200069162685, -0.000000000000000000, -0.9351131265310288487 ) ) ;
#110556=FACE_OUTER_BOUND ( 'NONE', #100858, .T. ) ;
#110557=ORIENTED_EDGE ( 'NONE', *, *, #109785, .T. ) ;
#110558=PLANE ( 'NONE',  #16431 ) ;
#110560=DIRECTION ( 'NONE',  ( -0.000000000000000000, 0.000000000000000000, 1.000000000000000000 ) ) ;
#110563=LINE ( 'NONE', #66391, #136564 ) ;
#110564=LINE ( 'NONE', #44672, #101817 ) ;
#110565=LINE ( 'NONE', #21452, #1272 ) ;
#110566=ORIENTED_EDGE ( 'NONE', *, *, #59959, .T. ) ;
#110567=DIRECTION ( 'NONE',  ( -0.6830127018922181881, 0.6830127018922202975, -0.2588190451025214056 ) ) ;
#110568=LINE ( 'NONE', #33779, #98590 ) ;
#110572=VECTOR ( 'NONE', #25576, 1000.000000000000000 ) ;
#110573=ORIENTED_EDGE ( 'NONE', *, *, #12983, .T. ) ;
#110574=ORIENTED_EDGE ( 'NONE', *, *, #68377, .T. ) ;
#110577=ORIENTED_EDGE ( 'NONE', *, *, #55450, .F. ) ;
#110578=DIRECTION ( 'NONE',  ( -0.000000000000000000, 0.3543493200069153248, 0.9351131265310292928 ) ) ;
#110579=EDGE_CURVE ( 'NONE', #120738, #95284, #77472, .T. ) ;
#110580=CARTESIAN_POINT ( 'NONE',  ( 4.499999999999966249, 16.77039438581780217, 0.4657186855307644535 ) ) ;
#110583=CARTESIAN_POINT ( 'NONE',  ( 12.08314806772922978, 21.75929247661549937, 7.311836541448077931 ) ) ;
#110584=ORIENTED_EDGE ( 'NONE', *, *, #130304, .T. ) ;
#110585=ORIENTED_EDGE ( 'NONE', *, *, #22718, .T. ) ;
#110586=PLANE ( 'NONE',  #44658 ) ;
#110587=EDGE_CURVE ( 'NONE', #94901, #97018, #142009, .T. ) ;
#110588=ADVANCED_FACE ( 'NONE', ( #76013 ), #31798, .F. ) ;
#110589=VERTEX_POINT ( 'NONE', #43392 ) ;
#110590=DIRECTION ( 'NONE',  ( -0.7071067811865486830, -0.7071067811865464625, 0.000000000000000000 ) ) ;
#110591=LINE ( 'NONE', #12003, #68819 ) ;
#110592=CARTESIAN_POINT ( 'NONE',  ( 24.75720643176650171, 22.22500000000000142, 27.61581905502973555 ) ) ;
#110593=VERTEX_POINT ( 'NONE', #131830 ) ;
#110595=FACE_BOUND ( 'NONE', #55856, .T. ) ;
#110597=CARTESIAN_POINT ( 'NONE',  ( -66.29974487139159578, -27.71228299555252406, 4.000000000000000000 ) ) ;
#110600=AXIS2_PLACEMENT_3D ( 'NONE', #41290, #52865, #73238 ) ;
#110604=ORIENTED_EDGE ( 'NONE', *, *, #102721, .T. ) ;
#110605=EDGE_LOOP ( 'NONE', ( #28996, #132182, #138317, #129616 ) ) ;
#110607=VERTEX_POINT ( 'NONE', #22308 ) ;
#110608=ADVANCED_FACE ( 'NONE', ( #11431 ), #55709, .T. ) ;
#110609=ORIENTED_EDGE ( 'NONE', *, *, #130594, .F. ) ;
#110610=DIRECTION ( 'NONE',  ( -0.7071067811865486830, -0.7071067811865464625, 0.000000000000000000 ) ) ;
#110611=EDGE_CURVE ( 'NONE', #29818, #41501, #123825, .T. ) ;
#110612=LINE ( 'NONE', #99031, #128793 ) ;
#110615=LINE ( 'NONE', #23635, #41440 ) ;
#110616=CARTESIAN_POINT ( 'NONE',  ( 39.18398860626899705, 28.73617430169814568, 5.000000000000000000 ) ) ;
#110617=FACE_BOUND ( 'NONE', #96240, .T. ) ;
#110618=DIRECTION ( 'NONE',  ( -0.7071067811865486830, -0.7071067811865464625, 0.000000000000000000 ) ) ;
#110619=CARTESIAN_POINT ( 'NONE',  ( -45.29974487139158867, -27.71228299555237840, 4.000000000000000000 ) ) ;
#110620=DIRECTION ( 'NONE',  ( 0.7071067811865486830, -0.7071067811865464625, -0.000000000000000000 ) ) ;
#110621=EDGE_CURVE ( 'NONE', #13795, #27559, #113626, .T. ) ;
#110623=ORIENTED_EDGE ( 'NONE', *, *, #102274, .F. ) ;
#110625=FACE_OUTER_BOUND ( 'NONE', #127041, .T. ) ;
#110628=ORIENTED_EDGE ( 'NONE', *, *, #50992, .F. ) ;
#110630=EDGE_CURVE ( 'NONE', #52088, #68553, #135420, .T. ) ;
#110631=ORIENTED_EDGE ( 'NONE', *, *, #81799, .F. ) ;
#110632=CARTESIAN_POINT ( 'NONE',  ( 1.499999999999994449, -7.420205493532897378, -2.617629953481250382 ) ) ;
#110633=EDGE_CURVE ( 'NONE', #104452, #64492, #1281, .T. ) ;
#110637=DIRECTION ( 'NONE',  ( 0.7071067811865486830, -0.7071067811865464625, -0.000000000000000000 ) ) ;
#110638=ORIENTED_EDGE ( 'NONE', *, *, #141244, .T. ) ;
#110639=DIRECTION ( 'NONE',  ( -0.7071067811865487940, 0.7071067811865463515, 0.000000000000000000 ) ) ;
#110640=EDGE_CURVE ( 'NONE', #13412, #58969, #68734, .T. ) ;
#110641=DIRECTION ( 'NONE',  ( -0.6830127018922181881, 0.6830127018922202975, -0.2588190451025214056 ) ) ;
#110642=CARTESIAN_POINT ( 'NONE',  ( -26.99999999999980815, -7.447814304570759880, 5.000000000000000000 ) ) ;
#110643=CARTESIAN_POINT ( 'NONE',  ( 54.48921356237310221, -27.52281430457093236, 5.000000000000000000 ) ) ;
#110644=EDGE_LOOP ( 'NONE', ( #85585, #75668, #27430, #69337 ) ) ;
#110646=VERTEX_POINT ( 'NONE', #101331 ) ;
#110647=ORIENTED_EDGE ( 'NONE', *, *, #87003, .F. ) ;
#110648=EDGE_LOOP ( 'NONE', ( #100292, #10131, #140830, #123606 ) ) ;
#110650=LINE ( 'NONE', #55611, #9799 ) ;
#110651=VECTOR ( 'NONE', #68423, 1000.000000000000000 ) ;
#110653=ORIENTED_EDGE ( 'NONE', *, *, #119105, .F. ) ;
#110655=CARTESIAN_POINT ( 'NONE',  ( -45.48921356237309510, -27.52281430457087197, 5.000000000000000000 ) ) ;
#110657=VECTOR ( 'NONE', #93727, 1000.000000000000227 ) ;
#110658=VECTOR ( 'NONE', #32573, 1000.000000000000000 ) ;
#110659=VECTOR ( 'NONE', #7318, 999.9999999999998863 ) ;
#110661=FACE_OUTER_BOUND ( 'NONE', #90888, .T. ) ;
#110665=ORIENTED_EDGE ( 'NONE', *, *, #118015, .T. ) ;
#110666=VERTEX_POINT ( 'NONE', #112921 ) ;
#110667=EDGE_CURVE ( 'NONE', #52975, #40545, #48377, .T. ) ;
#110668=ORIENTED_EDGE ( 'NONE', *, *, #14057, .T. ) ;
#110671=DIRECTION ( 'NONE',  ( -0.7071067811865487940, 0.7071067811865463515, 0.000000000000000000 ) ) ;
#110672=DIRECTION ( 'NONE',  ( -0.7071067811865487940, 0.7071067811865463515, 0.000000000000000000 ) ) ;
#110673=DIRECTION ( 'NONE',  ( 0.7071067811865486830, -0.7071067811865464625, -0.000000000000000000 ) ) ;
#110674=LINE ( 'NONE', #133898, #87331 ) ;
#110676=LINE ( 'NONE', #22951, #85894 ) ;
#110677=ORIENTED_EDGE ( 'NONE', *, *, #140711, .T. ) ;
#110679=ORIENTED_EDGE ( 'NONE', *, *, #17458, .F. ) ;
#110680=VECTOR ( 'NONE', #82574, 1000.000000000000000 ) ;
#110682=VERTEX_POINT ( 'NONE', #25916 ) ;
#110683=VECTOR ( 'NONE', #135860, 999.9999999999998863 ) ;
#110684=LINE ( 'NONE', #65104, #90010 ) ;
#110685=FACE_OUTER_BOUND ( 'NONE', #141437, .T. ) ;
#110688=CARTESIAN_POINT ( 'NONE',  ( 0.7928932188134528714, 6.759292476615656575, 5.000000000000000000 ) ) ;
#110689=CARTESIAN_POINT ( 'NONE',  ( 25.49999999999982947, 8.319652575858409449, -8.582050562765768831 ) ) ;
#110690=EDGE_LOOP ( 'NONE', ( #125345, #22195, #20448, #24573 ) ) ;
#110691=EDGE_CURVE ( 'NONE', #536, #22939, #57865, .T. ) ;
#110692=AXIS2_PLACEMENT_3D ( 'NONE', #1340, #34722, #101390 ) ;
#110694=CARTESIAN_POINT ( 'NONE',  ( 20.99999999999985434, -22.06887692260758982, 4.000000000000000000 ) ) ;
#110695=ORIENTED_EDGE ( 'NONE', *, *, #57784, .F. ) ;
#110696=( BOUNDED_CURVE ( )  B_SPLINE_CURVE ( 3, ( #15776, #112991, #49202, #71654 ),
 .UNSPECIFIED., .F., .F. ) 
 B_SPLINE_CURVE_WITH_KNOTS ( ( 4, 4 ),
 ( 1.610468072580459209, 1.654543780452488067 ),
 .UNSPECIFIED. ) 
 CURVE ( )  GEOMETRIC_REPRESENTATION_ITEM ( )  RATIONAL_B_SPLINE_CURVE ( ( 1.000000000000000000, 0.9998381175498711748, 0.9998381175498711748, 1.000000000000000000 ) ) 
 REPRESENTATION_ITEM ( '' )  );
#110697=EDGE_CURVE ( 'NONE', #3334, #43398, #25186, .T. ) ;
#110701=ADVANCED_FACE ( 'NONE', ( #81761 ), #69442, .F. ) ;
#110704=DIRECTION ( 'NONE',  ( 0.7071067811865487940, 0.7071067811865463515, -0.000000000000000000 ) ) ;
#110709=DIRECTION ( 'NONE',  ( 0.7071067811865487940, -0.7071067811865463515, 0.000000000000000000 ) ) ;
#110710=VERTEX_POINT ( 'NONE', #2720 ) ;
#110714=LINE ( 'NONE', #109322, #134721 ) ;
#110715=ORIENTED_EDGE ( 'NONE', *, *, #18606, .F. ) ;
#110717=DIRECTION ( 'NONE',  ( -0.7071067811865486830, -0.7071067811865464625, 0.000000000000000000 ) ) ;
#110718=CARTESIAN_POINT ( 'NONE',  ( -63.29974487139158867, -27.71228299555250274, 4.000000000000000000 ) ) ;
#110719=PLANE ( 'NONE',  #123435 ) ;
#110721=ADVANCED_FACE ( 'NONE', ( #47714 ), #125955, .F. ) ;
#110722=PLANE ( 'NONE',  #91448 ) ;
#110723=FACE_OUTER_BOUND ( 'NONE', #138342, .T. ) ;
#110724=DIRECTION ( 'NONE',  ( -0.000000000000000000, -0.000000000000000000, 1.000000000000000000 ) ) ;
#110725=LINE ( 'NONE', #95058, #9134 ) ;
#110727=CARTESIAN_POINT ( 'NONE',  ( 17.81601139373099940, 28.73617430169775133, 5.000000000000000000 ) ) ;
#110731=LINE ( 'NONE', #55695, #73174 ) ;
#110734=FACE_OUTER_BOUND ( 'NONE', #120127, .T. ) ;
#110735=ORIENTED_EDGE ( 'NONE', *, *, #40111, .T. ) ;
#110736=VERTEX_POINT ( 'NONE', #1966 ) ;
#110737=VERTEX_POINT ( 'NONE', #45567 ) ;
#110739=EDGE_LOOP ( 'NONE', ( #53934, #112367, #74606, #90675 ) ) ;
#110740=DIRECTION ( 'NONE',  ( 0.6830127018922180770, -0.6830127018922204085, -0.2588190451025213501 ) ) ;
#110741=EDGE_CURVE ( 'NONE', #131451, #118193, #91877, .T. ) ;
#110742=LINE ( 'NONE', #68046, #43391 ) ;
#110743=DIRECTION ( 'NONE',  ( 0.7071067811865486830, -0.7071067811865464625, -0.000000000000000000 ) ) ;
#110746=CARTESIAN_POINT ( 'NONE',  ( 8.999999999999936051, -19.22509904557635707, 1.855685503482199294 ) ) ;
#110747=CARTESIAN_POINT ( 'NONE',  ( 39.18398860626899705, 28.73617430169814568, 5.000000000000000000 ) ) ;
#110748=ADVANCED_FACE ( 'NONE', ( #79647 ), #36101, .F. ) ;
#110749=ADVANCED_FACE ( 'NONE', ( #90464 ), #91209, .F. ) ;
#110751=EDGE_LOOP ( 'NONE', ( #40617, #84337, #124432, #33745 ) ) ;
#110752=DIRECTION ( 'NONE',  ( -0.3543493200069162685, -0.000000000000000000, -0.9351131265310288487 ) ) ;
#110754=VECTOR ( 'NONE', #56492, 1000.000000000000000 ) ;
#110756=VECTOR ( 'NONE', #12377, 1000.000000000000000 ) ;
#110757=EDGE_CURVE ( 'NONE', #109724, #73565, #139705, .T. ) ;
#110758=ORIENTED_EDGE ( 'NONE', *, *, #81574, .T. ) ;
#110759=ORIENTED_EDGE ( 'NONE', *, *, #4528, .F. ) ;
#110761=ORIENTED_EDGE ( 'NONE', *, *, #10399, .T. ) ;
#110762=CARTESIAN_POINT ( 'NONE',  ( -15.31657961132780166, -6.740707523384212863, 11.88629033278127878 ) ) ;
#110764=VECTOR ( 'NONE', #24413, 999.9999999999998863 ) ;
#110765=CARTESIAN_POINT ( 'NONE',  ( 17.29289321881333663, 11.25929247661560062, 5.000000000000000000 ) ) ;
#110766=CARTESIAN_POINT ( 'NONE',  ( 34.92499999999998295, -21.72500000000000142, 5.000000000000000000 ) ) ;
#110767=VECTOR ( 'NONE', #104699, 1000.000000000000000 ) ;
#110768=LINE ( 'NONE', #98493, #73458 ) ;
#110769=CARTESIAN_POINT ( 'NONE',  ( 12.85005128541016894, -8.240707523384193323, 17.25253755692241953 ) ) ;
#110772=ORIENTED_EDGE ( 'NONE', *, *, #131628, .F. ) ;
#110773=EDGE_LOOP ( 'NONE', ( #75759, #69022, #20398, #1820 ) ) ;
#110774=EDGE_CURVE ( 'NONE', #57808, #125073, #95441, .T. ) ;
#110776=ORIENTED_EDGE ( 'NONE', *, *, #118092, .F. ) ;
#110777=VERTEX_POINT ( 'NONE', #29468 ) ;
#110778=VECTOR ( 'NONE', #138002, 1000.000000000000000 ) ;
#110779=EDGE_CURVE ( 'NONE', #118230, #84933, #6250, .T. ) ;
#110780=VECTOR ( 'NONE', #72105, 1000.000000000000000 ) ;
#110781=DIRECTION ( 'NONE',  ( -0.000000000000000000, 0.000000000000000000, 1.000000000000000000 ) ) ;
#110782=ORIENTED_EDGE ( 'NONE', *, *, #129977, .F. ) ;
#110783=LINE ( 'NONE', #25223, #117683 ) ;
#110784=LINE ( 'NONE', #80361, #30999 ) ;
#110785=CARTESIAN_POINT ( 'NONE',  ( -3.183988606268992161, 28.73617430169789699, 5.000000000000000000 ) ) ;
#110786=LINE ( 'NONE', #133310, #55441 ) ;
#110787=AXIS2_PLACEMENT_3D ( 'NONE', #35388, #136085, #112905 ) ;
#110788=PLANE ( 'NONE',  #88368 ) ;
#110789=ORIENTED_EDGE ( 'NONE', *, *, #59601, .T. ) ;
#110790=AXIS2_PLACEMENT_3D ( 'NONE', #35338, #79580, #68672 ) ;
#110791=CARTESIAN_POINT ( 'NONE',  ( 29.67183060077626422, -18.74070752338408852, 4.000000000000000000 ) ) ;
#110792=EDGE_LOOP ( 'NONE', ( #99377, #4048, #109797, #50097 ) ) ;
#110794=ORIENTED_EDGE ( 'NONE', *, *, #6760, .F. ) ;
#110796=ORIENTED_EDGE ( 'NONE', *, *, #26490, .T. ) ;
#110797=CARTESIAN_POINT ( 'NONE',  ( 21.32816939922338051, 11.25929247661560240, 4.000000000000000000 ) ) ;
#110798=ORIENTED_EDGE ( 'NONE', *, *, #110917, .F. ) ;
#110799=VERTEX_POINT ( 'NONE', #72323 ) ;
#110800=VECTOR ( 'NONE', #7839, 1000.000000000000227 ) ;
#110801=VERTEX_POINT ( 'NONE', #60729 ) ;
#110802=PLANE ( 'NONE',  #97440 ) ;
#110804=DIRECTION ( 'NONE',  ( -0.6830127018922180770, -0.6830127018922204085, -0.2588190451025213501 ) ) ;
#110806=CARTESIAN_POINT ( 'NONE',  ( 26.67183060077628198, 2.259292476615699652, 4.000000000000000000 ) ) ;
#110807=CARTESIAN_POINT ( 'NONE',  ( 2.816011393730999401, 28.73617430169785436, 5.000000000000000000 ) ) ;
#110808=PLANE ( 'NONE',  #121998 ) ;
#110809=VECTOR ( 'NONE', #67784, 1000.000000000000114 ) ;
#110811=DIRECTION ( 'NONE',  ( -0.7071067811865486830, -0.7071067811865464625, 0.000000000000000000 ) ) ;
#110812=ORIENTED_EDGE ( 'NONE', *, *, #82825, .F. ) ;
#110814=DIRECTION ( 'NONE',  ( 1.000000000000000000, 0.000000000000000000, 0.000000000000000000 ) ) ;
#110815=EDGE_LOOP ( 'NONE', ( #115390, #66714, #23418, #67620 ) ) ;
#110817=VERTEX_POINT ( 'NONE', #73028 ) ;
#110819=ORIENTED_EDGE ( 'NONE', *, *, #39444, .T. ) ;
#110822=DIRECTION ( 'NONE',  ( -0.6830127018922181881, 0.6830127018922202975, -0.2588190451025214056 ) ) ;
#110823=LINE ( 'NONE', #40113, #82023 ) ;
#110824=CARTESIAN_POINT ( 'NONE',  ( -6.183988606268994381, 28.73617430169791476, 5.000000000000000000 ) ) ;
#110825=ORIENTED_EDGE ( 'NONE', *, *, #98008, .F. ) ;
#110826=LINE ( 'NONE', #12256, #23275 ) ;
#110827=EDGE_LOOP ( 'NONE', ( #137900, #13113, #49353, #14151 ) ) ;
#110828=FACE_OUTER_BOUND ( 'NONE', #28031, .T. ) ;
#110830=ORIENTED_EDGE ( 'NONE', *, *, #26668, .T. ) ;
#110832=CARTESIAN_POINT ( 'NONE',  ( 27.29974487139158512, -27.71228299555225405, 4.000000000000000000 ) ) ;
#110833=CARTESIAN_POINT ( 'NONE',  ( 14.99999999999989697, 18.08204922493374411, 0.9627537363044524898 ) ) ;
#110834=ORIENTED_EDGE ( 'NONE', *, *, #8486, .F. ) ;
#110835=ORIENTED_EDGE ( 'NONE', *, *, #10399, .F. ) ;
#110836=EDGE_CURVE ( 'NONE', #32567, #4325, #117179, .T. ) ;
#110837=ORIENTED_EDGE ( 'NONE', *, *, #41876, .T. ) ;
#110838=CARTESIAN_POINT ( 'NONE',  ( -33.18398860626899705, 28.73617430169810305, 5.000000000000000000 ) ) ;
#110839=FACE_OUTER_BOUND ( 'NONE', #74916, .T. ) ;
#110841=DIRECTION ( 'NONE',  ( -0.7071067811865487940, 0.7071067811865463515, -0.000000000000000000 ) ) ;
#110842=CARTESIAN_POINT ( 'NONE',  ( -13.49999999999990763, -5.947814304570766986, 5.000000000000000000 ) ) ;
#110843=ORIENTED_EDGE ( 'NONE', *, *, #91631, .T. ) ;
#110844=CARTESIAN_POINT ( 'NONE',  ( -13.11547925347946908, 3.815643823912585386, 4.000000000000000000 ) ) ;
#110845=CARTESIAN_POINT ( 'NONE',  ( 15.56584921360887108, 8.021612662230191759, 4.000000000000000000 ) ) ;
#110847=EDGE_CURVE ( 'NONE', #5368, #80916, #137545, .T. ) ;
#110848=ORIENTED_EDGE ( 'NONE', *, *, #138569, .T. ) ;
#110850=VECTOR ( 'NONE', #141469, 1000.000000000000000 ) ;
#110851=VECTOR ( 'NONE', #119197, 1000.000000000000000 ) ;
#110852=AXIS2_PLACEMENT_3D ( 'NONE', #141756, #42458, #130885 ) ;
#110854=LINE ( 'NONE', #133377, #28509 ) ;
#110856=VECTOR ( 'NONE', #40584, 999.9999999999998863 ) ;
#110857=ADVANCED_FACE ( 'NONE', ( #128788 ), #106287, .F. ) ;
#110859=ORIENTED_EDGE ( 'NONE', *, *, #77823, .F. ) ;
#110860=VERTEX_POINT ( 'NONE', #84592 ) ;
#110861=EDGE_CURVE ( 'NONE', #132460, #92286, #82449, .T. ) ;
#110862=EDGE_CURVE ( 'NONE', #43034, #43627, #62849, .T. ) ;
#110864=CARTESIAN_POINT ( 'NONE',  ( -5.010880286539445727, -22.02621442084248216, 4.990779571109223767 ) ) ;
#110865=ORIENTED_EDGE ( 'NONE', *, *, #77283, .F. ) ;
#110866=LINE ( 'NONE', #35526, #113783 ) ;
#110868=ADVANCED_FACE ( 'NONE', ( #51251 ), #127360, .F. ) ;
#110870=DIRECTION ( 'NONE',  ( -0.7071067811865487940, 0.7071067811865463515, 0.000000000000000000 ) ) ;
#110871=DIRECTION ( 'NONE',  ( 0.7071067811865486830, -0.7071067811865464625, -0.000000000000000000 ) ) ;
#110872=DIRECTION ( 'NONE',  ( 0.7071067811865487940, -0.7071067811865463515, 0.000000000000000000 ) ) ;
#110873=FACE_OUTER_BOUND ( 'NONE', #98394, .T. ) ;
#110874=EDGE_CURVE ( 'NONE', #66673, #63704, #128103, .T. ) ;
#110875=DIRECTION ( 'NONE',  ( -0.6830127018922180770, -0.6830127018922204085, -0.2588190451025213501 ) ) ;
#110876=DIRECTION ( 'NONE',  ( 0.7071067811865487940, 0.7071067811865463515, -0.000000000000000000 ) ) ;
#110877=DIRECTION ( 'NONE',  ( 0.6830127018922181881, 0.6830127018922202975, -0.2588190451025214056 ) ) ;
#110879=DIRECTION ( 'NONE',  ( -0.7071067811865487940, 0.7071067811865463515, -0.000000000000000000 ) ) ;
#110880=VECTOR ( 'NONE', #66694, 999.9999999999998863 ) ;
#110881=DIRECTION ( 'NONE',  ( -0.000000000000000000, 0.000000000000000000, 1.000000000000000000 ) ) ;
#110883=FACE_OUTER_BOUND ( 'NONE', #141828, .T. ) ;
#110884=DIRECTION ( 'NONE',  ( 0.6830127018922181881, 0.6830127018922202975, -0.2588190451025214056 ) ) ;
#110885=VERTEX_POINT ( 'NONE', #28060 ) ;
#110886=ORIENTED_EDGE ( 'NONE', *, *, #82722, .F. ) ;
#110888=EDGE_CURVE ( 'NONE', #49530, #86149, #50525, .T. ) ;
#110889=VECTOR ( 'NONE', #48726, 1000.000000000000000 ) ;
#110890=VERTEX_POINT ( 'NONE', #49118 ) ;
#110891=ORIENTED_EDGE ( 'NONE', *, *, #84447, .T. ) ;
#110893=LINE ( 'NONE', #714, #8567 ) ;
#110894=LINE ( 'NONE', #101469, #39325 ) ;
#110895=ORIENTED_EDGE ( 'NONE', *, *, #10947, .T. ) ;
#110896=VECTOR ( 'NONE', #16998, 999.9999999999998863 ) ;
#110897=LINE ( 'NONE', #120334, #46396 ) ;
#110898=VECTOR ( 'NONE', #109121, 1000.000000000000227 ) ;
#110899=DIRECTION ( 'NONE',  ( 0.7071067811865487940, 0.7071067811865463515, -0.000000000000000000 ) ) ;
#110900=AXIS2_PLACEMENT_3D ( 'NONE', #46942, #78100, #57078 ) ;
#110901=CARTESIAN_POINT ( 'NONE',  ( -26.99999999999981526, 12.83542986846994793, -1.025386466790308315 ) ) ;
#110902=CARTESIAN_POINT ( 'NONE',  ( -27.29974487139158512, -27.71228299555225405, 4.000000000000000000 ) ) ;
#110903=ORIENTED_EDGE ( 'NONE', *, *, #94161, .F. ) ;
#110904=CARTESIAN_POINT ( 'NONE',  ( 19.49999999999985789, -2.777013188829488666, 4.549262955118046570 ) ) ;
#110906=VECTOR ( 'NONE', #42498, 1000.000000000000000 ) ;
#110907=EDGE_CURVE ( 'NONE', #100760, #111455, #93312, .T. ) ;
#110909=DIRECTION ( 'NONE',  ( 0.6830127018922180770, -0.6830127018922204085, -0.2588190451025213501 ) ) ;
#110912=LINE ( 'NONE', #1439, #116294 ) ;
#110913=EDGE_LOOP ( 'NONE', ( #135484, #125325, #106908, #18046 ) ) ;
#110914=ORIENTED_EDGE ( 'NONE', *, *, #90288, .F. ) ;
#110916=ORIENTED_EDGE ( 'NONE', *, *, #23536, .F. ) ;
#110917=EDGE_CURVE ( 'NONE', #62936, #93695, #61445, .T. ) ;
#110918=CARTESIAN_POINT ( 'NONE',  ( -23.99999999999984013, -13.97847968911262484, -0.1324546996127346499 ) ) ;
#110920=PLANE ( 'NONE',  #87326 ) ;
#110921=DIRECTION ( 'NONE',  ( -0.7071067811865487940, 0.7071067811865463515, 0.000000000000000000 ) ) ;
#110925=ORIENTED_EDGE ( 'NONE', *, *, #69926, .F. ) ;
#110926=EDGE_CURVE ( 'NONE', #118674, #129502, #5567, .T. ) ;
#110927=ORIENTED_EDGE ( 'NONE', *, *, #65099, .F. ) ;
#110928=DIRECTION ( 'NONE',  ( 1.000000000000000000, 0.000000000000000000, 0.000000000000000000 ) ) ;
#110929=DIRECTION ( 'NONE',  ( 0.6830127018922181881, 0.6830127018922202975, -0.2588190451025214056 ) ) ;
#110930=EDGE_CURVE ( 'NONE', #24156, #42638, #54132, .T. ) ;
#110931=ADVANCED_FACE ( 'NONE', ( #54822 ), #121478, .F. ) ;
#110932=ORIENTED_EDGE ( 'NONE', *, *, #59045, .T. ) ;
#110935=ORIENTED_EDGE ( 'NONE', *, *, #115950, .T. ) ;
#110936=CARTESIAN_POINT ( 'NONE',  ( -75.18398860626899705, 28.73617430169839793, 5.000000000000000000 ) ) ;
#110937=CARTESIAN_POINT ( 'NONE',  ( -32.99999999999977973, 4.965500833774297185, -4.007596771432582194 ) ) ;
#110938=DIRECTION ( 'NONE',  ( 0.6830127018922181881, 0.6830127018922202975, -0.2588190451025214056 ) ) ;
#110940=CARTESIAN_POINT ( 'NONE',  ( 20.67183060077632462, -6.740707523384212863, 4.000000000000000000 ) ) ;
#110941=ORIENTED_EDGE ( 'NONE', *, *, #110151, .F. ) ;
#110942=EDGE_CURVE ( 'NONE', #26469, #87228, #99725, .T. ) ;
#110944=EDGE_LOOP ( 'NONE', ( #16325, #17595, #10705 ) ) ;
#110945=VERTEX_POINT ( 'NONE', #397 ) ;
#110946=ORIENTED_EDGE ( 'NONE', *, *, #20749, .T. ) ;
#110948=LINE ( 'NONE', #69655, #18666 ) ;
#110949=EDGE_CURVE ( 'NONE', #109570, #134004, #19320, .T. ) ;
#110950=ORIENTED_EDGE ( 'NONE', *, *, #109132, .T. ) ;
#110951=DIRECTION ( 'NONE',  ( -0.6830127018922180770, -0.6830127018922204085, -0.2588190451025213501 ) ) ;
#110952=CARTESIAN_POINT ( 'NONE',  ( 0.000000000000000000, 0.000000000000000000, 5.000000000000000000 ) ) ;
#110956=AXIS2_PLACEMENT_3D ( 'NONE', #66232, #33615, #99531 ) ;
#110957=( BOUNDED_CURVE ( )  B_SPLINE_CURVE ( 3, ( #103634, #72511, #59477, #115206 ),
 .UNSPECIFIED., .F., .T. ) 
 B_SPLINE_CURVE_WITH_KNOTS ( ( 4, 4 ),
 ( 0.4286956587950772612, 0.5111536932531051125 ),
 .UNSPECIFIED. ) 
 CURVE ( )  GEOMETRIC_REPRESENTATION_ITEM ( )  RATIONAL_B_SPLINE_CURVE ( ( 1.000000000000000000, 0.9994334696367943582, 0.9994334696367943582, 1.000000000000000000 ) ) 
 REPRESENTATION_ITEM ( '' )  );
#110958=DIRECTION ( 'NONE',  ( -0.7071067811865486830, -0.7071067811865464625, 0.000000000000000000 ) ) ;
#110960=EDGE_CURVE ( 'NONE', #65337, #73728, #129492, .T. ) ;
#110961=FACE_BOUND ( 'NONE', #45293, .T. ) ;
#110964=DIRECTION ( 'NONE',  ( 1.000000000000000000, 0.000000000000000000, 0.000000000000000000 ) ) ;
#110965=LINE ( 'NONE', #45077, #25411 ) ;
#110966=EDGE_CURVE ( 'NONE', #53919, #10232, #31633, .T. ) ;
#110967=ORIENTED_EDGE ( 'NONE', *, *, #56181, .F. ) ;
#110970=ORIENTED_EDGE ( 'NONE', *, *, #72717, .F. ) ;
#110971=AXIS2_PLACEMENT_3D ( 'NONE', #32475, #20138, #9228 ) ;
#110973=ORIENTED_EDGE ( 'NONE', *, *, #9915, .F. ) ;
#110976=AXIS2_PLACEMENT_3D ( 'NONE', #114443, #136198, #91980 ) ;
#110977=PLANE ( 'NONE',  #125088 ) ;
#110979=DIRECTION ( 'NONE',  ( 0.7071067811865487940, 0.7071067811865463515, 0.000000000000000000 ) ) ;
#110981=PLANE ( 'NONE',  #69998 ) ;
#110982=LINE ( 'NONE', #55946, #31984 ) ;
#110983=AXIS2_PLACEMENT_3D ( 'NONE', #14968, #59939, #49065 ) ;
#110986=AXIS2_PLACEMENT_3D ( 'NONE', #23762, #12854, #1949 ) ;
#110987=EDGE_CURVE ( 'NONE', #109374, #2192, #53370, .T. ) ;
#110988=PLANE ( 'NONE',  #20096 ) ;
#110989=CARTESIAN_POINT ( 'NONE',  ( 5.700255128608413102, -27.71228299555201957, 4.000000000000000000 ) ) ;
#110990=DIRECTION ( 'NONE',  ( -0.000000000000000000, -0.3543493200069152693, 0.9351131265310292928 ) ) ;
#110991=DIRECTION ( 'NONE',  ( 0.3543493200069162685, -0.000000000000000000, -0.9351131265310288487 ) ) ;
#110993=EDGE_LOOP ( 'NONE', ( #50388, #12777, #74716 ) ) ;
#110994=ORIENTED_EDGE ( 'NONE', *, *, #46020, .T. ) ;
#110995=ORIENTED_EDGE ( 'NONE', *, *, #89621, .T. ) ;
#110998=ORIENTED_EDGE ( 'NONE', *, *, #19455, .F. ) ;
#110999=VECTOR ( 'NONE', #50306, 1000.000000000000000 ) ;
#111000=VECTOR ( 'NONE', #64198, 1000.000000000000000 ) ;
#111001=ORIENTED_EDGE ( 'NONE', *, *, #127989, .T. ) ;
#111002=DIRECTION ( 'NONE',  ( 0.7071067811865487940, -0.7071067811865463515, 0.000000000000000000 ) ) ;
#111003=DIRECTION ( 'NONE',  ( -0.6830127018922180770, -0.6830127018922204085, -0.2588190451025213501 ) ) ;
#111004=EDGE_CURVE ( 'NONE', #29906, #87047, #118620, .T. ) ;
#111005=VECTOR ( 'NONE', #60500, 1000.000000000000227 ) ;
#111006=DIRECTION ( 'NONE',  ( -0.000000000000000000, -0.3543493200069152693, 0.9351131265310292928 ) ) ;
#111007=EDGE_LOOP ( 'NONE', ( #12650, #78415, #36092, #2117, #135137 ) ) ;
#111009=LINE ( 'NONE', #142948, #136609 ) ;
#111010=DIRECTION ( 'NONE',  ( -0.000000000000000000, -0.3543493200069152693, 0.9351131265310292928 ) ) ;
#111012=PLANE ( 'NONE',  #131852 ) ;
#111013=ORIENTED_EDGE ( 'NONE', *, *, #68554, .F. ) ;
#111015=CARTESIAN_POINT ( 'NONE',  ( 29.99999999999979750, -19.22509904557633575, 1.855685503482247034 ) ) ;
#111016=CARTESIAN_POINT ( 'NONE',  ( 9.489213562373095101, -27.52281430457062328, 5.000000000000000000 ) ) ;
#111017=VECTOR ( 'NONE', #65200, 1000.000000000000227 ) ;
#111018=DIRECTION ( 'NONE',  ( 0.000000000000000000, 0.000000000000000000, 1.000000000000000000 ) ) ;
#111019=ORIENTED_EDGE ( 'NONE', *, *, #3423, .F. ) ;
#111020=CARTESIAN_POINT ( 'NONE',  ( 29.20710678118634007, 3.759292476615678336, 5.000000000000000000 ) ) ;
#111021=ORIENTED_EDGE ( 'NONE', *, *, #60367, .T. ) ;
#111023=DIRECTION ( 'NONE',  ( 0.6830127018922181881, 0.6830127018922202975, -0.2588190451025214056 ) ) ;
#111024=ORIENTED_EDGE ( 'NONE', *, *, #42239, .F. ) ;
#111025=CARTESIAN_POINT ( 'NONE',  ( 1.771493228613341575, 20.25929247661551003, 7.808871592221773739 ) ) ;
#111026=FACE_OUTER_BOUND ( 'NONE', #75270, .T. ) ;
#111027=ORIENTED_EDGE ( 'NONE', *, *, #66758, .T. ) ;
#111028=DIRECTION ( 'NONE',  ( -0.000000000000000000, -0.3543493200069152693, 0.9351131265310292928 ) ) ;
#111029=ORIENTED_EDGE ( 'NONE', *, *, #19160, .T. ) ;
#111030=DIRECTION ( 'NONE',  ( -0.7071067811865487940, 0.7071067811865463515, -0.000000000000000000 ) ) ;
#111032=ORIENTED_EDGE ( 'NONE', *, *, #14963, .T. ) ;
#111034=VERTEX_POINT ( 'NONE', #20011 ) ;
#111036=CARTESIAN_POINT ( 'NONE',  ( 45.29974487139158867, -27.71228299555237840, 4.000000000000000000 ) ) ;
#111037=VERTEX_POINT ( 'NONE', #141833 ) ;
#111038=CARTESIAN_POINT ( 'NONE',  ( 6.299744871391586898, -27.71228299555210484, 4.000000000000000000 ) ) ;
#111039=ADVANCED_FACE ( 'NONE', ( #86736 ), #130960, .F. ) ;
#111040=EDGE_CURVE ( 'NONE', #89322, #128406, #133112, .T. ) ;
#111041=DIRECTION ( 'NONE',  ( 0.6830127018922180770, -0.6830127018922204085, -0.2588190451025213501 ) ) ;
#111042=DIRECTION ( 'NONE',  ( -0.7071067811865486830, 0.7071067811865464625, 0.000000000000000000 ) ) ;
#111043=EDGE_CURVE ( 'NONE', #37138, #114295, #91706, .T. ) ;
#111044=ORIENTED_EDGE ( 'NONE', *, *, #19864, .F. ) ;
#111045=DIRECTION ( 'NONE',  ( -0.000000000000000000, 0.000000000000000000, 1.000000000000000000 ) ) ;
#111046=EDGE_CURVE ( 'NONE', #42984, #70961, #124343, .T. ) ;
#111049=DIRECTION ( 'NONE',  ( 0.7071067811865487940, 0.7071067811865463515, 0.000000000000000000 ) ) ;
#111053=VERTEX_POINT ( 'NONE', #3934 ) ;
#111054=ORIENTED_EDGE ( 'NONE', *, *, #72093, .F. ) ;
#111057=EDGE_LOOP ( 'NONE', ( #89444, #12923, #120289, #53937 ) ) ;
#111058=EDGE_LOOP ( 'NONE', ( #89115, #78056, #3644, #119219 ) ) ;
#111059=CARTESIAN_POINT ( 'NONE',  ( 20.32505044418271467, 22.22500000000000142, 25.93630946864303866 ) ) ;
#111061=VECTOR ( 'NONE', #77013, 1000.000000000000000 ) ;
#111063=VECTOR ( 'NONE', #67403, 1000.000000000000000 ) ;
#111064=VERTEX_POINT ( 'NONE', #112053 ) ;
#111066=FACE_OUTER_BOUND ( 'NONE', #2193, .T. ) ;
#111068=ADVANCED_FACE ( 'NONE', ( #135930 ), #68563, .F. ) ;
#111069=DIRECTION ( 'NONE',  ( -0.6830127018922181881, 0.6830127018922202975, -0.2588190451025214056 ) ) ;
#111070=DIRECTION ( 'NONE',  ( 0.7071067811865486830, -0.7071067811865464625, -0.000000000000000000 ) ) ;
#111072=ORIENTED_EDGE ( 'NONE', *, *, #4720, .F. ) ;
#111073=FACE_OUTER_BOUND ( 'NONE', #140244, .T. ) ;
#111075=DIRECTION ( 'NONE',  ( -0.000000000000000000, -0.3543493200069152693, 0.9351131265310292928 ) ) ;
#111076=VECTOR ( 'NONE', #37479, 1000.000000000000000 ) ;
#111078=PLANE ( 'NONE',  #26553 ) ;
#111079=EDGE_CURVE ( 'NONE', #18068, #139716, #112750, .T. ) ;
#111080=DIRECTION ( 'NONE',  ( -0.7071067811865486830, -0.7071067811865464625, 0.000000000000000000 ) ) ;
#111081=DIRECTION ( 'NONE',  ( -0.7071067811865487940, 0.7071067811865463515, 0.000000000000000000 ) ) ;
#111083=DIRECTION ( 'NONE',  ( -0.000000000000000000, -0.3543493200069152693, 0.9351131265310292928 ) ) ;
#111084=CARTESIAN_POINT ( 'NONE',  ( -3.005480084712505828, 28.92564299267936079, 4.000000000000000000 ) ) ;
#111085=ORIENTED_EDGE ( 'NONE', *, *, #7640, .F. ) ;
#111086=VERTEX_POINT ( 'NONE', #101153 ) ;
#111088=DIRECTION ( 'NONE',  ( -0.000000000000000000, 0.000000000000000000, 1.000000000000000000 ) ) ;
#111089=AXIS2_PLACEMENT_3D ( 'NONE', #40687, #76909, #75459 ) ;
#111090=CARTESIAN_POINT ( 'NONE',  ( -21.72281430457044493, -21.72500000000000142, 5.000000000000000000 ) ) ;
#111091=VERTEX_POINT ( 'NONE', #1798 ) ;
#111093=CARTESIAN_POINT ( 'NONE',  ( 54.18398860626899705, 28.73617430169825226, 5.000000000000000000 ) ) ;
#111094=VECTOR ( 'NONE', #53351, 999.9999999999998863 ) ;
#111096=ORIENTED_EDGE ( 'NONE', *, *, #93949, .F. ) ;
#111099=VERTEX_POINT ( 'NONE', #22850 ) ;
#111101=DIRECTION ( 'NONE',  ( -0.3543493200069162685, -0.000000000000000000, -0.9351131265310288487 ) ) ;
#111102=VECTOR ( 'NONE', #116636, 1000.000000000000227 ) ;
#111103=CARTESIAN_POINT ( 'NONE',  ( -18.70710678118640402, -12.74070752338415780, 5.000000000000000000 ) ) ;
#111104=LINE ( 'NONE', #121290, #95262 ) ;
#111105=CARTESIAN_POINT ( 'NONE',  ( -34.82816939922329169, 21.75929247661549937, 4.000000000000000000 ) ) ;
#111107=LINE ( 'NONE', #34295, #115952 ) ;
#111108=ORIENTED_EDGE ( 'NONE', *, *, #81548, .F. ) ;
#111109=VECTOR ( 'NONE', #50059, 1000.000000000000000 ) ;
#111112=CARTESIAN_POINT ( 'NONE',  ( 39.48921356237310221, -27.52281430457082934, 5.000000000000000000 ) ) ;
#111113=DIRECTION ( 'NONE',  ( 0.6830127018922180770, -0.6830127018922204085, -0.2588190451025213501 ) ) ;
#111115=CARTESIAN_POINT ( 'NONE',  ( 21.48921356237309155, -27.52281430457070499, 5.000000000000000000 ) ) ;
#111117=EDGE_CURVE ( 'NONE', #142920, #81300, #36608, .T. ) ;
#111118=ORIENTED_EDGE ( 'NONE', *, *, #139782, .F. ) ;
#111122=DIRECTION ( 'NONE',  ( 0.7071067811865487940, -0.7071067811865463515, 0.000000000000000000 ) ) ;
#111123=EDGE_CURVE ( 'NONE', #80245, #94584, #100460, .T. ) ;
#111124=CARTESIAN_POINT ( 'NONE',  ( 34.17183060077623225, -17.24070752338410628, 4.000000000000000000 ) ) ;
#111126=ORIENTED_EDGE ( 'NONE', *, *, #53526, .F. ) ;
#111127=VECTOR ( 'NONE', #26940, 1000.000000000000000 ) ;
#111128=CARTESIAN_POINT ( 'NONE',  ( 3.489213562373097322, -27.52281430457057709, 5.000000000000000000 ) ) ;
#111130=EDGE_LOOP ( 'NONE', ( #74930, #87499, #48753, #84075 ) ) ;
#111131=EDGE_CURVE ( 'NONE', #74472, #113129, #78701, .T. ) ;
#111132=CARTESIAN_POINT ( 'NONE',  ( 23.51078643762690490, -27.52281430457038880, 5.000000000000000000 ) ) ;
#111134=LINE ( 'NONE', #32926, #23739 ) ;
#111135=CARTESIAN_POINT ( 'NONE',  ( 0.2997448713915885632, -27.71228299555206220, 4.000000000000000000 ) ) ;
#111137=LINE ( 'NONE', #89414, #39644 ) ;
#111138=EDGE_CURVE ( 'NONE', #39654, #12388, #37306, .T. ) ;
#111139=FACE_BOUND ( 'NONE', #95105, .T. ) ;
#111140=CARTESIAN_POINT ( 'NONE',  ( -63.29974487139158867, -27.71228299555250274, 4.000000000000000000 ) ) ;
#111141=FACE_OUTER_BOUND ( 'NONE', #94957, .T. ) ;
#111143=CARTESIAN_POINT ( 'NONE',  ( 36.29974487139159578, -27.71228299555231445, 4.000000000000000000 ) ) ;
#111144=ORIENTED_EDGE ( 'NONE', *, *, #109865, .F. ) ;
#111146=FACE_OUTER_BOUND ( 'NONE', #129960, .T. ) ;
#111148=ORIENTED_EDGE ( 'NONE', *, *, #50698, .F. ) ;
#111149=EDGE_CURVE ( 'NONE', #1315, #2318, #13410, .T. ) ;
#111150=EDGE_LOOP ( 'NONE', ( #17227, #82931, #26039, #15528 ) ) ;
#111152=ORIENTED_EDGE ( 'NONE', *, *, #135104, .T. ) ;
#111153=LINE ( 'NONE', #56851, #117020 ) ;
#111155=ORIENTED_EDGE ( 'NONE', *, *, #137941, .T. ) ;
#111156=LINE ( 'NONE', #66980, #132393 ) ;
#111158=EDGE_CURVE ( 'NONE', #105448, #142261, #80857, .T. ) ;
#111159=DIRECTION ( 'NONE',  ( -0.000000000000000000, 0.3543493200069153248, 0.9351131265310292928 ) ) ;
#111160=VECTOR ( 'NONE', #41318, 1000.000000000000000 ) ;
#111161=FACE_OUTER_BOUND ( 'NONE', #114671, .T. ) ;
#111162=VECTOR ( 'NONE', #73096, 1000.000000000000000 ) ;
#111163=ADVANCED_FACE ( 'NONE', ( #6796 ), #39493, .T. ) ;
#111164=FACE_OUTER_BOUND ( 'NONE', #114351, .T. ) ;
#111166=LINE ( 'NONE', #129537, #140789 ) ;
#111167=DIRECTION ( 'NONE',  ( 0.7071067811865487940, 0.7071067811865463515, 0.000000000000000000 ) ) ;
#111168=FACE_OUTER_BOUND ( 'NONE', #99510, .T. ) ;
#111169=VECTOR ( 'NONE', #118437, 1000.000000000000227 ) ;
#111170=ORIENTED_EDGE ( 'NONE', *, *, #38770, .F. ) ;
#111171=AXIS2_PLACEMENT_3D ( 'NONE', #117422, #18099, #62382 ) ;
#111174=VERTEX_POINT ( 'NONE', #106120 ) ;
#111175=LINE ( 'NONE', #89441, #119152 ) ;
#111176=LINE ( 'NONE', #56151, #132334 ) ;
#111177=ORIENTED_EDGE ( 'NONE', *, *, #127528, .F. ) ;
#111178=VECTOR ( 'NONE', #42597, 1000.000000000000000 ) ;
#111179=ORIENTED_EDGE ( 'NONE', *, *, #50492, .T. ) ;
#111180=ORIENTED_EDGE ( 'NONE', *, *, #41550, .T. ) ;
#111181=EDGE_CURVE ( 'NONE', #130625, #110318, #83727, .T. ) ;
#111183=ORIENTED_EDGE ( 'NONE', *, *, #12528, .F. ) ;
#111184=VECTOR ( 'NONE', #72647, 1000.000000000000000 ) ;
#111185=DIRECTION ( 'NONE',  ( -0.3543493200069162685, -0.000000000000000000, -0.9351131265310288487 ) ) ;
#111186=CARTESIAN_POINT ( 'NONE',  ( 1.499999999999990896, 11.52377502935403619, -1.522421517564086502 ) ) ;
#111190=DIRECTION ( 'NONE',  ( -0.7071067811865486830, -0.7071067811865464625, 0.000000000000000000 ) ) ;
#111191=CARTESIAN_POINT ( 'NONE',  ( -20.00492477221182241, -5.240707523384225297, 12.38332538355500745 ) ) ;
#111192=AXIS2_PLACEMENT_3D ( 'NONE', #121783, #124656, #22462 ) ;
#111193=CARTESIAN_POINT ( 'NONE',  ( -5.994519915287488843, 28.92564299267942118, 4.000000000000000000 ) ) ;
#111194=CARTESIAN_POINT ( 'NONE',  ( 8.125146193092287916, -14.24070752338413470, 9.401115078912640755 ) ) ;
#111195=ORIENTED_EDGE ( 'NONE', *, *, #58973, .F. ) ;
#111196=ORIENTED_EDGE ( 'NONE', *, *, #36107, .T. ) ;
#111197=CARTESIAN_POINT ( 'NONE',  ( -6.489213562373093325, -27.52281430457059841, 5.000000000000000000 ) ) ;
#111198=DIRECTION ( 'NONE',  ( 0.7071067811865486830, -0.7071067811865464625, -0.000000000000000000 ) ) ;
#111199=ORIENTED_EDGE ( 'NONE', *, *, #20898, .T. ) ;
#111201=PLANE ( 'NONE',  #34224 ) ;
#111203=VECTOR ( 'NONE', #54513, 1000.000000000000000 ) ;
#111204=ORIENTED_EDGE ( 'NONE', *, *, #140677, .F. ) ;
#111205=VECTOR ( 'NONE', #23368, 1000.000000000000000 ) ;
#111206=CARTESIAN_POINT ( 'NONE',  ( -23.67183060077630330, 8.259292476615630818, 4.000000000000000000 ) ) ;
#111208=LINE ( 'NONE', #135844, #42562 ) ;
#111209=DIRECTION ( 'NONE',  ( -0.000000000000000000, -0.3543493200069152693, 0.9351131265310292928 ) ) ;
#111211=CARTESIAN_POINT ( 'NONE',  ( -18.32816939922340183, -9.740707523384182664, 4.000000000000000000 ) ) ;
#111212=DIRECTION ( 'NONE',  ( -0.7071067811865486830, -0.7071067811865464625, 0.000000000000000000 ) ) ;
#111213=LINE ( 'NONE', #78617, #33247 ) ;
#111215=ORIENTED_EDGE ( 'NONE', *, *, #52806, .F. ) ;
#111216=VECTOR ( 'NONE', #94103, 999.9999999999998863 ) ;
#111217=PLANE ( 'NONE',  #67518 ) ;
#111218=VERTEX_POINT ( 'NONE', #103983 ) ;
#111220=CARTESIAN_POINT ( 'NONE',  ( 27.48921356237309155, -27.52281430457074762, 5.000000000000000000 ) ) ;
#111221=LINE ( 'NONE', #119940, #92182 ) ;
#111222=EDGE_CURVE ( 'NONE', #114427, #131551, #73314, .T. ) ;
#111223=ORIENTED_EDGE ( 'NONE', *, *, #115466, .F. ) ;
#111224=VECTOR ( 'NONE', #41725, 1000.000000000000000 ) ;
#111225=LINE ( 'NONE', #11917, #73948 ) ;
#111226=DIRECTION ( 'NONE',  ( -0.6830127018922180770, -0.6830127018922204085, -0.2588190451025213501 ) ) ;
#111227=DIRECTION ( 'NONE',  ( -0.6830127018922180770, -0.6830127018922204085, -0.2588190451025213501 ) ) ;
#111228=EDGE_CURVE ( 'NONE', #36893, #22361, #138806, .T. ) ;
#111229=ORIENTED_EDGE ( 'NONE', *, *, #887, .F. ) ;
#111232=EDGE_CURVE ( 'NONE', #99152, #41615, #49671, .T. ) ;
#111235=CARTESIAN_POINT ( 'NONE',  ( -34.92500000000001137, -21.18334561358935986, 4.500000000000000888 ) ) ;
#111239=LINE ( 'NONE', #80610, #6774 ) ;
#111241=DIRECTION ( 'NONE',  ( 0.7071067811865486830, -0.7071067811865464625, -0.000000000000000000 ) ) ;
#111242=ORIENTED_EDGE ( 'NONE', *, *, #35061, .T. ) ;
#111243=ORIENTED_EDGE ( 'NONE', *, *, #112708, .F. ) ;
#111245=CARTESIAN_POINT ( 'NONE',  ( -8.999999999999921840, -16.44781430457067373, 5.000000000000000000 ) ) ;
#111247=CARTESIAN_POINT ( 'NONE',  ( 0.000000000000000000, -10.77435723561695902, -9.972017380717231205 ) ) ;
#111248=ADVANCED_FACE ( 'NONE', ( #137373 ), #73544, .F. ) ;
#111250=EDGE_CURVE ( 'NONE', #62294, #135455, #113084, .T. ) ;
#111252=DIRECTION ( 'NONE',  ( 1.000000000000000000, 0.000000000000000000, 0.000000000000000000 ) ) ;
#111253=ORIENTED_EDGE ( 'NONE', *, *, #81699, .T. ) ;
#111254=VERTEX_POINT ( 'NONE', #81582 ) ;
#111255=LINE ( 'NONE', #34432, #34771 ) ;
#111256=DIRECTION ( 'NONE',  ( 0.7071067811865487940, -0.7071067811865463515, 0.000000000000000000 ) ) ;
#111260=ADVANCED_FACE ( 'NONE', ( #84435 ), #128629, .T. ) ;
#111261=DIRECTION ( 'NONE',  ( -0.7071067811865486830, -0.7071067811865464625, 0.000000000000000000 ) ) ;
#111263=DIRECTION ( 'NONE',  ( 0.7071067811865487940, -0.7071067811865463515, 0.000000000000000000 ) ) ;
#111264=CARTESIAN_POINT ( 'NONE',  ( -24.48921356237309510, -27.52281430457072631, 5.000000000000000000 ) ) ;
#111265=VERTEX_POINT ( 'NONE', #72147 ) ;
#111267=DIRECTION ( 'NONE',  ( 0.7071067811865486830, -0.7071067811865464625, -0.000000000000000000 ) ) ;
#111268=CARTESIAN_POINT ( 'NONE',  ( 69.29974487139159578, -27.71228299555254537, 4.000000000000000000 ) ) ;
#111269=LINE ( 'NONE', #88852, #17362 ) ;
#111270=EDGE_CURVE ( 'NONE', #49451, #44722, #29301, .T. ) ;
#111271=ORIENTED_EDGE ( 'NONE', *, *, #24125, .T. ) ;
#111272=AXIS2_PLACEMENT_3D ( 'NONE', #141773, #44629, #23534 ) ;
#111273=DIRECTION ( 'NONE',  ( 0.7071067811865486830, -0.7071067811865464625, -0.000000000000000000 ) ) ;
#111275=ORIENTED_EDGE ( 'NONE', *, *, #97819, .F. ) ;
#111277=PLANE ( 'NONE',  #60608 ) ;
#111279=LINE ( 'NONE', #88130, #19982 ) ;
#111280=EDGE_CURVE ( 'NONE', #24661, #18835, #38065, .T. ) ;
#111281=ORIENTED_EDGE ( 'NONE', *, *, #38939, .F. ) ;
#111282=VECTOR ( 'NONE', #22583, 1000.000000000000000 ) ;
#111283=VECTOR ( 'NONE', #127302, 999.9999999999998863 ) ;
#111285=VECTOR ( 'NONE', #54467, 1000.000000000000000 ) ;
#111287=LINE ( 'NONE', #77288, #107787 ) ;
#111288=LINE ( 'NONE', #67099, #6968 ) ;
#111289=FACE_OUTER_BOUND ( 'NONE', #95307, .T. ) ;
#111290=CARTESIAN_POINT ( 'NONE',  ( -15.48921356237309510, -27.52281430457066236, 5.000000000000000000 ) ) ;
#111291=ORIENTED_EDGE ( 'NONE', *, *, #112424, .F. ) ;
#111292=CARTESIAN_POINT ( 'NONE',  ( -5.999999999999963585, 14.87792677143808362, -11.06722581663441218 ) ) ;
#111293=CARTESIAN_POINT ( 'NONE',  ( 8.994519915287490619, 28.92564299267944250, 4.000000000000000000 ) ) ;
#111297=VERTEX_POINT ( 'NONE', #104723 ) ;
#111298=EDGE_LOOP ( 'NONE', ( #71828, #94931, #88203, #38364 ) ) ;
#111300=ORIENTED_EDGE ( 'NONE', *, *, #23521, .F. ) ;
#111301=VECTOR ( 'NONE', #56659, 1000.000000000000000 ) ;
#111303=CARTESIAN_POINT ( 'NONE',  ( 16.49999999999988276, 12.43112307739205669, 4.000000000000000000 ) ) ;
#111304=LINE ( 'NONE', #13408, #13237 ) ;
#111307=DIRECTION ( 'NONE',  ( 1.000000000000000000, 0.000000000000000000, 0.000000000000000000 ) ) ;
#111308=CARTESIAN_POINT ( 'NONE',  ( 51.18398860626899705, 28.73617430169823095, 5.000000000000000000 ) ) ;
#111309=ORIENTED_EDGE ( 'NONE', *, *, #52655, .T. ) ;
#111310=VERTEX_POINT ( 'NONE', #41608 ) ;
#111311=CARTESIAN_POINT ( 'NONE',  ( -45.18398860626900415, 28.73617430169818832, 5.000000000000000000 ) ) ;
#111314=EDGE_LOOP ( 'NONE', ( #73428, #55102, #48360, #14979 ) ) ;
#111315=AXIS2_PLACEMENT_3D ( 'NONE', #64790, #119838, #30746 ) ;
#111316=ADVANCED_FACE ( 'NONE', ( #63408 ), #119851, .T. ) ;
#111317=DIRECTION ( 'NONE',  ( -1.000000000000000000, 0.000000000000000000, -0.000000000000000000 ) ) ;
#111319=DIRECTION ( 'NONE',  ( 0.7071067811865487940, -0.7071067811865463515, 0.000000000000000000 ) ) ;
#111320=DIRECTION ( 'NONE',  ( -0.7071067811865486830, 0.7071067811865464625, 0.000000000000000000 ) ) ;
#111321=AXIS2_PLACEMENT_3D ( 'NONE', #10855, #56593, #55122 ) ;
#111322=ORIENTED_EDGE ( 'NONE', *, *, #48619, .T. ) ;
#111323=EDGE_CURVE ( 'NONE', #11268, #142123, #64084, .T. ) ;
#111324=FACE_BOUND ( 'NONE', #24784, .T. ) ;
#111325=CARTESIAN_POINT ( 'NONE',  ( -17.81601139373099940, 28.73617430169775133, 5.000000000000000000 ) ) ;
#111326=CARTESIAN_POINT ( 'NONE',  ( 72.18398860626899705, 28.73617430169837661, 5.000000000000000000 ) ) ;
#111327=CARTESIAN_POINT ( 'NONE',  ( -10.49999999999992895, -5.568876922607761237, 4.000000000000000000 ) ) ;
#111328=DIRECTION ( 'NONE',  ( 0.3543493200069162685, -0.000000000000000000, -0.9351131265310288487 ) ) ;
#111329=DIRECTION ( 'NONE',  ( 1.000000000000000000, 0.000000000000000000, 0.000000000000000000 ) ) ;
#111330=EDGE_LOOP ( 'NONE', ( #7296, #67158, #93513, #5610, #125141 ) ) ;
#111331=VECTOR ( 'NONE', #100920, 1000.000000000000000 ) ;
#111332=VERTEX_POINT ( 'NONE', #21294 ) ;
#111334=ORIENTED_EDGE ( 'NONE', *, *, #104569, .F. ) ;
#111337=ORIENTED_EDGE ( 'NONE', *, *, #38779, .F. ) ;
#111338=CARTESIAN_POINT ( 'NONE',  ( -25.49999999999982236, -14.70932175296479549, -11.46312253303831064 ) ) ;
#111341=ORIENTED_EDGE ( 'NONE', *, *, #29379, .F. ) ;
#111342=DIRECTION ( 'NONE',  ( 0.6830127018922180770, -0.6830127018922204085, -0.2588190451025213501 ) ) ;
#111343=LINE ( 'NONE', #90315, #119029 ) ;
#111344=ADVANCED_FACE ( 'NONE', ( #9682 ), #30010, .F. ) ;
#111345=CARTESIAN_POINT ( 'NONE',  ( 29.12514619309216712, -14.24070752338413293, 9.401115078912591017 ) ) ;
#111347=CARTESIAN_POINT ( 'NONE',  ( -66.48921356237309510, -27.52281430457101763, 5.000000000000000000 ) ) ;
#111348=CARTESIAN_POINT ( 'NONE',  ( 6.489213562373093325, -27.52281430457059841, 5.000000000000000000 ) ) ;
#111350=DIRECTION ( 'NONE',  ( -0.6830127018922181881, 0.6830127018922202975, -0.2588190451025214056 ) ) ;
#111351=VERTEX_POINT ( 'NONE', #54650 ) ;
#111352=LINE ( 'NONE', #46145, #963 ) ;
#111353=DIRECTION ( 'NONE',  ( 0.7071067811865487940, 0.7071067811865463515, -0.000000000000000000 ) ) ;
#111354=VERTEX_POINT ( 'NONE', #119164 ) ;
#111355=EDGE_CURVE ( 'NONE', #22968, #83246, #40907, .T. ) ;
#111356=VERTEX_POINT ( 'NONE', #98836 ) ;
#111357=ADVANCED_FACE ( 'NONE', ( #85821 ), #65553, .F. ) ;
#111360=VECTOR ( 'NONE', #105218, 999.9999999999998863 ) ;
#111362=PLANE ( 'NONE',  #92906 ) ;
#111365=PLANE ( 'NONE',  #88844 ) ;
#111366=LINE ( 'NONE', #78771, #68852 ) ;
#111367=ORIENTED_EDGE ( 'NONE', *, *, #67327, .T. ) ;
#111368=CARTESIAN_POINT ( 'NONE',  ( 28.82816939922333077, -2.240707523384257716, 4.000000000000000000 ) ) ;
#111371=EDGE_LOOP ( 'NONE', ( #59082, #139039, #73899, #110946 ) ) ;
#111372=EDGE_CURVE ( 'NONE', #90846, #118847, #129321, .T. ) ;
#111375=VECTOR ( 'NONE', #54001, 1000.000000000000000 ) ;
#111376=CARTESIAN_POINT ( 'NONE',  ( 29.91508676806220990, -12.74070752338414536, 18.74364270924360909 ) ) ;
#111378=ORIENTED_EDGE ( 'NONE', *, *, #142075, .T. ) ;
#111379=LINE ( 'NONE', #4710, #108265 ) ;
#111380=VERTEX_POINT ( 'NONE', #19147 ) ;
#111381=ORIENTED_EDGE ( 'NONE', *, *, #17629, .F. ) ;
#111382=VERTEX_POINT ( 'NONE', #130060 ) ;
#111383=VECTOR ( 'NONE', #91306, 1000.000000000000000 ) ;
#111384=AXIS2_PLACEMENT_3D ( 'NONE', #11942, #35887, #113393 ) ;
#111385=VECTOR ( 'NONE', #31215, 1000.000000000000000 ) ;
#111386=VECTOR ( 'NONE', #100800, 1000.000000000000000 ) ;
#111387=VECTOR ( 'NONE', #103028, 1000.000000000000000 ) ;
#111388=DIRECTION ( 'NONE',  ( 0.6830127018922181881, 0.6830127018922202975, -0.2588190451025214056 ) ) ;
#111389=CARTESIAN_POINT ( 'NONE',  ( 1.499999999999994449, -9.462702396501011748, -9.474982329943516746 ) ) ;
#111390=DIRECTION ( 'NONE',  ( -0.6830127018922181881, 0.6830127018922202975, -0.2588190451025214056 ) ) ;
#111391=ADVANCED_FACE ( 'NONE', ( #143067 ), #43758, .F. ) ;
#111392=CIRCLE ( 'NONE', #51302, 5.968999999999998529 ) ;
#111393=ORIENTED_EDGE ( 'NONE', *, *, #119098, .T. ) ;
#111394=LINE ( 'NONE', #79552, #132992 ) ;
#111396=CARTESIAN_POINT ( 'NONE',  ( -7.499999999999940492, 7.087461875839172087, 4.000000000000000000 ) ) ;
#111397=EDGE_CURVE ( 'NONE', #61782, #123748, #19848, .T. ) ;
#111398=LINE ( 'NONE', #134618, #96875 ) ;
#111399=VECTOR ( 'NONE', #46124, 1000.000000000000000 ) ;
#111400=DIRECTION ( 'NONE',  ( -0.6830127018922181881, 0.6830127018922202975, -0.2588190451025214056 ) ) ;
#111401=ORIENTED_EDGE ( 'NONE', *, *, #114012, .T. ) ;
#111402=ADVANCED_FACE ( 'NONE', ( #42355 ), #86565, .F. ) ;
#111403=EDGE_LOOP ( 'NONE', ( #49418, #140148, #77861, #84578 ) ) ;
#111404=ORIENTED_EDGE ( 'NONE', *, *, #135573, .F. ) ;
#111405=FACE_OUTER_BOUND ( 'NONE', #69705, .T. ) ;
#111407=DIRECTION ( 'NONE',  ( -0.7071067811865486830, -0.7071067811865464625, -0.000000000000000000 ) ) ;
#111408=DIRECTION ( 'NONE',  ( 0.7071067811865486830, -0.7071067811865464625, -0.000000000000000000 ) ) ;
#111409=EDGE_CURVE ( 'NONE', #82317, #17208, #32167, .T. ) ;
#111411=EDGE_CURVE ( 'NONE', #117995, #27223, #941, .T. ) ;
#111412=VECTOR ( 'NONE', #108267, 999.9999999999998863 ) ;
#111413=VECTOR ( 'NONE', #30369, 999.9999999999998863 ) ;
#111414=CARTESIAN_POINT ( 'NONE',  ( 16.17183060077637791, 9.759292476615634371, 4.000000000000000000 ) ) ;
#111415=LINE ( 'NONE', #25112, #58826 ) ;
#111416=CARTESIAN_POINT ( 'NONE',  ( 12.79333936457838483, 21.75929247661549937, 4.998822639870715179 ) ) ;
#111417=DIRECTION ( 'NONE',  ( 0.7071067811865487940, 0.7071067811865463515, 0.000000000000000000 ) ) ;
#111418=VECTOR ( 'NONE', #3472, 1000.000000000000000 ) ;
#111419=ORIENTED_EDGE ( 'NONE', *, *, #140053, .F. ) ;
#111420=CARTESIAN_POINT ( 'NONE',  ( -34.17183060077623225, -2.240707523384260824, 4.000000000000000000 ) ) ;
#111421=ORIENTED_EDGE ( 'NONE', *, *, #39546, .T. ) ;
#111423=AXIS2_PLACEMENT_3D ( 'NONE', #15668, #125194, #34617 ) ;
#111424=VERTEX_POINT ( 'NONE', #68406 ) ;
#111425=LINE ( 'NONE', #121585, #115436 ) ;
#111427=ORIENTED_EDGE ( 'NONE', *, *, #17798, .T. ) ;
#111428=EDGE_CURVE ( 'NONE', #5925, #34100, #57226, .T. ) ;
#111429=AXIS2_PLACEMENT_3D ( 'NONE', #67432, #113033, #1402 ) ;
#111430=EDGE_CURVE ( 'NONE', #14195, #57153, #137741, .T. ) ;
#111431=LINE ( 'NONE', #56397, #55616 ) ;
#111432=LINE ( 'NONE', #46219, #908 ) ;
#111433=EDGE_LOOP ( 'NONE', ( #36564, #78221, #90586, #77360 ) ) ;
#111434=LINE ( 'NONE', #109298, #48513 ) ;
#111435=ORIENTED_EDGE ( 'NONE', *, *, #115762, .F. ) ;
#111436=DIRECTION ( 'NONE',  ( -0.7071067811865487940, 0.7071067811865463515, -0.000000000000000000 ) ) ;
#111438=ORIENTED_EDGE ( 'NONE', *, *, #69630, .T. ) ;
#111439=CARTESIAN_POINT ( 'NONE',  ( 6.722814304570563948, -21.72499999999999432, 5.000000000000000000 ) ) ;
#111443=DIRECTION ( 'NONE',  ( -0.7071067811865486830, -0.7071067811865464625, -0.000000000000000000 ) ) ;
#111445=CARTESIAN_POINT ( 'NONE',  ( -3.489213562373097322, -27.52281430457057709, 5.000000000000000000 ) ) ;
#111448=VECTOR ( 'NONE', #89545, 1000.000000000000000 ) ;
#111449=DIRECTION ( 'NONE',  ( 0.7071067811865486830, -0.7071067811865464625, -0.000000000000000000 ) ) ;
#111450=ADVANCED_FACE ( 'NONE', ( #24149 ), #112585, .T. ) ;
#111451=DIRECTION ( 'NONE',  ( 0.7071067811865487940, 0.7071067811865463515, 0.000000000000000000 ) ) ;
#111452=AXIS2_PLACEMENT_3D ( 'NONE', #12813, #1212, #45495 ) ;
#111454=ORIENTED_EDGE ( 'NONE', *, *, #91513, .T. ) ;
#111455=VERTEX_POINT ( 'NONE', #82635 ) ;
#111456=CARTESIAN_POINT ( 'NONE',  ( 42.48921356237308800, -27.52281430457085065, 5.000000000000000000 ) ) ;
#111459=VECTOR ( 'NONE', #131718, 999.9999999999998863 ) ;
#111461=LINE ( 'NONE', #3394, #90306 ) ;
#111462=EDGE_CURVE ( 'NONE', #40635, #134689, #27512, .T. ) ;
#111463=CARTESIAN_POINT ( 'NONE',  ( 17.81601139373099940, 28.73617430169775133, 5.000000000000000000 ) ) ;
#111464=AXIS2_PLACEMENT_3D ( 'NONE', #27606, #17448, #39220 ) ;
#111465=DIRECTION ( 'NONE',  ( 0.7071067811865487940, 0.7071067811865463515, 0.000000000000000000 ) ) ;
#111466=VERTEX_POINT ( 'NONE', #35777 ) ;
#111469=CARTESIAN_POINT ( 'NONE',  ( 5.999999999999960032, 4.965500833774338929, -4.007596771432669236 ) ) ;
#111470=DIRECTION ( 'NONE',  ( -0.7071067811865486830, 0.7071067811865464625, 0.000000000000000000 ) ) ;
#111471=PLANE ( 'NONE',  #93450 ) ;
#111472=CARTESIAN_POINT ( 'NONE',  ( 68.99451991528748351, 28.92564299267986172, 4.000000000000000000 ) ) ;
#111473=ADVANCED_FACE ( 'NONE', ( #44510 ), #33624, .F. ) ;
#111474=EDGE_LOOP ( 'NONE', ( #22958, #40642, #73048, #91086 ) ) ;
#111475=CARTESIAN_POINT ( 'NONE',  ( -29.67183060077625711, -15.74070752338412404, 4.000000000000000000 ) ) ;
#111476=EDGE_CURVE ( 'NONE', #61191, #30378, #38998, .T. ) ;
#111477=VECTOR ( 'NONE', #60300, 1000.000000000000000 ) ;
#111478=DIRECTION ( 'NONE',  ( -0.7071067811865486830, -0.7071067811865464625, -0.000000000000000000 ) ) ;
#111479=DIRECTION ( 'NONE',  ( 0.7071067811865487940, 0.7071067811865463515, 0.000000000000000000 ) ) ;
#111480=CARTESIAN_POINT ( 'NONE',  ( 17.20710678118642889, 9.759292476615620160, 5.000000000000000000 ) ) ;
#111481=VERTEX_POINT ( 'NONE', #77822 ) ;
#111482=ADVANCED_FACE ( 'NONE', ( #12544 ), #26813, .T. ) ;
#111484=ORIENTED_EDGE ( 'NONE', *, *, #14047, .T. ) ;
#111487=PLANE ( 'NONE',  #43988 ) ;
#111489=CARTESIAN_POINT ( 'NONE',  ( 39.29974487139159578, -27.71228299555233576, 4.000000000000000000 ) ) ;
#111490=DIRECTION ( 'NONE',  ( 0.6830127018922181881, 0.6830127018922202975, -0.2588190451025214056 ) ) ;
#111491=ORIENTED_EDGE ( 'NONE', *, *, #19671, .F. ) ;
#111492=VECTOR ( 'NONE', #53744, 1000.000000000000000 ) ;
#111493=CARTESIAN_POINT ( 'NONE',  ( 8.700255128608413102, -27.71228299555199825, 4.000000000000000000 ) ) ;
#111494=CARTESIAN_POINT ( 'NONE',  ( -12.29974487139158512, -27.71228299555214747, 4.000000000000000000 ) ) ;
#111495=AXIS2_PLACEMENT_3D ( 'NONE', #117583, #18269, #7409 ) ;
#111496=DIRECTION ( 'NONE',  ( -0.000000000000000000, -0.3543493200069152693, 0.9351131265310292928 ) ) ;
#111497=VECTOR ( 'NONE', #71419, 1000.000000000000000 ) ;
#111500=CARTESIAN_POINT ( 'NONE',  ( -6.938893903907228378E-15, -13.39766691384883579, -10.96608748226465835 ) ) ;
#111501=VECTOR ( 'NONE', #141223, 1000.000000000000000 ) ;
#111505=AXIS2_PLACEMENT_3D ( 'NONE', #113897, #24743, #136356 ) ;
#111506=ORIENTED_EDGE ( 'NONE', *, *, #43720, .F. ) ;
#111507=ORIENTED_EDGE ( 'NONE', *, *, #112539, .F. ) ;
#111508=DIRECTION ( 'NONE',  ( 0.7071067811865487940, 0.7071067811865463515, 0.000000000000000000 ) ) ;
#111509=LINE ( 'NONE', #134731, #121827 ) ;
#111510=DIRECTION ( 'NONE',  ( 0.7071067811865487940, 0.7071067811865463515, 0.000000000000000000 ) ) ;
#111512=LINE ( 'NONE', #33972, #48013 ) ;
#111514=DIRECTION ( 'NONE',  ( 0.6830127018922181881, 0.6830127018922202975, -0.2588190451025214056 ) ) ;
#111516=ORIENTED_EDGE ( 'NONE', *, *, #133768, .F. ) ;
#111517=VERTEX_POINT ( 'NONE', #90856 ) ;
#111518=CARTESIAN_POINT ( 'NONE',  ( -21.80077440930739030, -2.123201397992801276, 4.669108085256719498 ) ) ;
#111519=ORIENTED_EDGE ( 'NONE', *, *, #135081, .T. ) ;
#111521=ORIENTED_EDGE ( 'NONE', *, *, #111372, .T. ) ;
#111522=AXIS2_PLACEMENT_3D ( 'NONE', #10929, #89245, #75519 ) ;
#111524=DIRECTION ( 'NONE',  ( -0.7071067811865486830, -0.7071067811865464625, 0.000000000000000000 ) ) ;
#111526=CARTESIAN_POINT ( 'NONE',  ( 24.48921356237309510, -27.52281430457072631, 5.000000000000000000 ) ) ;
#111527=PLANE ( 'NONE',  #74996 ) ;
#111531=ORIENTED_EDGE ( 'NONE', *, *, #121105, .F. ) ;
#111532=DIRECTION ( 'NONE',  ( -0.000000000000000000, -0.3543493200069152693, 0.9351131265310292928 ) ) ;
#111533=ORIENTED_EDGE ( 'NONE', *, *, #66163, .F. ) ;
#111534=ADVANCED_FACE ( 'NONE', ( #11812 ), #56099, .F. ) ;
#111535=CARTESIAN_POINT ( 'NONE',  ( 5.999999999999957367, 16.55218569542900298, 5.000000000000000000 ) ) ;
#111536=VERTEX_POINT ( 'NONE', #45227 ) ;
#111537=CARTESIAN_POINT ( 'NONE',  ( 12.18398860626900060, 28.73617430169795739, 5.000000000000000000 ) ) ;
#111539=CARTESIAN_POINT ( 'NONE',  ( -36.48921356237310221, -27.52281430457080802, 5.000000000000000000 ) ) ;
#111541=ORIENTED_EDGE ( 'NONE', *, *, #94915, .F. ) ;
#111543=VECTOR ( 'NONE', #32949, 1000.000000000000000 ) ;
#111544=ORIENTED_EDGE ( 'NONE', *, *, #104328, .F. ) ;
#111545=DIRECTION ( 'NONE',  ( -0.000000000000000000, -0.3543493200069153248, 0.9351131265310292928 ) ) ;
#111546=CARTESIAN_POINT ( 'NONE',  ( 8.994519915287490619, 28.92564299267944250, 4.000000000000000000 ) ) ;
#111547=DIRECTION ( 'NONE',  ( 0.7071067811865487940, 0.7071067811865463515, 0.000000000000000000 ) ) ;
#111550=EDGE_CURVE ( 'NONE', #122875, #46067, #134352, .T. ) ;
#111551=LINE ( 'NONE', #11489, #11146 ) ;
#111552=AXIS2_PLACEMENT_3D ( 'NONE', #46458, #81939, #136993 ) ;
#111553=FACE_OUTER_BOUND ( 'NONE', #3712, .T. ) ;
#111554=VECTOR ( 'NONE', #96424, 1000.000000000000000 ) ;
#111555=DIRECTION ( 'NONE',  ( 0.000000000000000000, 0.000000000000000000, -1.000000000000000000 ) ) ;
#111558=ORIENTED_EDGE ( 'NONE', *, *, #92284, .F. ) ;
#111560=CARTESIAN_POINT ( 'NONE',  ( 6.707106781186501721, 11.25929247661560240, 5.000000000000000000 ) ) ;
#111562=VERTEX_POINT ( 'NONE', #139173 ) ;
#111563=ORIENTED_EDGE ( 'NONE', *, *, #4165, .T. ) ;
#111565=VECTOR ( 'NONE', #132119, 1000.000000000000227 ) ;
#111566=CARTESIAN_POINT ( 'NONE',  ( -18.29974487139159223, -27.71228299555219010, 4.000000000000000000 ) ) ;
#111568=ORIENTED_EDGE ( 'NONE', *, *, #64836, .T. ) ;
#111571=DIRECTION ( 'NONE',  ( -0.000000000000000000, 0.3543493200069153248, 0.9351131265310292928 ) ) ;
#111572=DIRECTION ( 'NONE',  ( 0.7071067811865487940, -0.7071067811865463515, 0.000000000000000000 ) ) ;
#111573=ORIENTED_EDGE ( 'NONE', *, *, #42304, .T. ) ;
#111575=EDGE_CURVE ( 'NONE', #70270, #101548, #18041, .T. ) ;
#111577=ADVANCED_FACE ( 'NONE', ( #83349 ), #16641, .F. ) ;
#111578=ORIENTED_EDGE ( 'NONE', *, *, #14738, .F. ) ;
#111579=( BOUNDED_CURVE ( )  B_SPLINE_CURVE ( 3, ( #12292, #121755, #79759, #113023 ),
 .UNSPECIFIED., .F., .T. ) 
 B_SPLINE_CURVE_WITH_KNOTS ( ( 4, 4 ),
 ( 2.779374508378134045, 4.199602562396863803 ),
 .UNSPECIFIED. ) 
 CURVE ( )  GEOMETRIC_REPRESENTATION_ITEM ( )  RATIONAL_B_SPLINE_CURVE ( ( 1.000000000000000000, 0.8388583629366570538, 0.8388583629366570538, 1.000000000000000000 ) ) 
 REPRESENTATION_ITEM ( '' )  );
#111580=CARTESIAN_POINT ( 'NONE',  ( -31.49999999999977973, -19.53360074219753884, 5.000000000000000000 ) ) ;
#111582=ORIENTED_EDGE ( 'NONE', *, *, #3777, .F. ) ;
#111584=DIRECTION ( 'NONE',  ( -0.7071067811865486830, 0.7071067811865464625, 0.000000000000000000 ) ) ;
#111585=DIRECTION ( 'NONE',  ( 0.6830127018922181881, 0.6830127018922202975, -0.2588190451025214056 ) ) ;
#111587=EDGE_CURVE ( 'NONE', #45393, #77014, #72515, .T. ) ;
#111588=DIRECTION ( 'NONE',  ( 0.6830127018922180770, -0.6830127018922204085, -0.2588190451025213501 ) ) ;
#111589=ORIENTED_EDGE ( 'NONE', *, *, #40467, .T. ) ;
#111590=ORIENTED_EDGE ( 'NONE', *, *, #7460, .T. ) ;
#111591=DIRECTION ( 'NONE',  ( -0.7071067811865486830, 0.7071067811865464625, 0.000000000000000000 ) ) ;
#111592=CARTESIAN_POINT ( 'NONE',  ( -34.92500000000001137, -22.22500000000000142, 4.000000000000000000 ) ) ;
#111593=DIRECTION ( 'NONE',  ( -0.7071067811865486830, -0.7071067811865464625, 0.000000000000000000 ) ) ;
#111594=AXIS2_PLACEMENT_3D ( 'NONE', #108184, #52403, #8844 ) ;
#111595=AXIS2_PLACEMENT_3D ( 'NONE', #92843, #79887, #45806 ) ;
#111596=CARTESIAN_POINT ( 'NONE',  ( -4.171830600776447184, 3.759292476615681888, 4.000000000000000000 ) ) ;
#111597=VECTOR ( 'NONE', #15890, 1000.000000000000000 ) ;
#111598=CARTESIAN_POINT ( 'NONE',  ( 15.29974487139158867, -27.71228299555216879, 4.000000000000000000 ) ) ;
#111599=ORIENTED_EDGE ( 'NONE', *, *, #84472, .T. ) ;
#111602=ADVANCED_FACE ( 'NONE', ( #63050 ), #86204, .T. ) ;
#111603=DIRECTION ( 'NONE',  ( 0.7071067811865486830, -0.7071067811865464625, -0.000000000000000000 ) ) ;
#111604=DIRECTION ( 'NONE',  ( -0.6830127018922181881, 0.6830127018922202975, -0.2588190451025214056 ) ) ;
#111606=ORIENTED_EDGE ( 'NONE', *, *, #19515, .F. ) ;
#111607=LINE ( 'NONE', #100734, #7344 ) ;
#111608=VECTOR ( 'NONE', #88123, 1000.000000000000000 ) ;
#111609=VECTOR ( 'NONE', #43185, 1000.000000000000000 ) ;
#111610=VECTOR ( 'NONE', #53955, 1000.000000000000000 ) ;
#111611=AXIS2_PLACEMENT_3D ( 'NONE', #69609, #77621, #113066 ) ;
#111613=EDGE_CURVE ( 'NONE', #115452, #16626, #28256, .T. ) ;
#111615=DIRECTION ( 'NONE',  ( -0.000000000000000000, -0.3543493200069152693, 0.9351131265310292928 ) ) ;
#111616=ORIENTED_EDGE ( 'NONE', *, *, #83690, .T. ) ;
#111618=ORIENTED_EDGE ( 'NONE', *, *, #105807, .F. ) ;
#111619=EDGE_CURVE ( 'NONE', #101569, #27362, #74626, .T. ) ;
#111620=PLANE ( 'NONE',  #86420 ) ;
#111621=CARTESIAN_POINT ( 'NONE',  ( 24.18398860626899705, 28.73617430169804265, 5.000000000000000000 ) ) ;
#111622=EDGE_LOOP ( 'NONE', ( #134653, #109608, #55130 ) ) ;
#111623=CARTESIAN_POINT ( 'NONE',  ( -42.29974487139158157, -27.71228299555235708, 4.000000000000000000 ) ) ;
#111625=CARTESIAN_POINT ( 'NONE',  ( -30.18398860626900060, 28.73617430169808173, 5.000000000000000000 ) ) ;
#111626=CARTESIAN_POINT ( 'NONE',  ( 3.005480084712505828, 28.92564299267936079, 4.000000000000000000 ) ) ;
#111627=DIRECTION ( 'NONE',  ( -0.000000000000000000, -0.3543493200069152693, 0.9351131265310292928 ) ) ;
#111628=EDGE_CURVE ( 'NONE', #53028, #82630, #7166, .T. ) ;
#111629=DIRECTION ( 'NONE',  ( -0.7071067811865487940, 0.7071067811865463515, 0.000000000000000000 ) ) ;
#111630=CARTESIAN_POINT ( 'NONE',  ( -12.12147316337139813, -20.24070752338407431, 7.412974875817818443 ) ) ;
#111631=FACE_OUTER_BOUND ( 'NONE', #2286, .T. ) ;
#111632=DIRECTION ( 'NONE',  ( -0.000000000000000000, -0.000000000000000000, 1.000000000000000000 ) ) ;
#111633=CARTESIAN_POINT ( 'NONE',  ( -22.96836484077793727, 2.259292476615697876, 13.77329220150631883 ) ) ;
#111635=DIRECTION ( 'NONE',  ( -0.7071067811865487940, 0.7071067811865463515, -0.000000000000000000 ) ) ;
#111636=CARTESIAN_POINT ( 'NONE',  ( 0.000000000000000000, 0.000000000000000000, 5.000000000000000000 ) ) ;
#111637=EDGE_CURVE ( 'NONE', #30838, #78485, #6435, .T. ) ;
#111638=CARTESIAN_POINT ( 'NONE',  ( 10.74845587132417890, -11.24070752338416490, 10.39518518046006790 ) ) ;
#111639=DIRECTION ( 'NONE',  ( -0.7071067811865486830, 0.7071067811865464625, 0.000000000000000000 ) ) ;
#111640=ORIENTED_EDGE ( 'NONE', *, *, #130147, .T. ) ;
#111641=AXIS2_PLACEMENT_3D ( 'NONE', #123149, #4126, #134753 ) ;
#111642=ORIENTED_EDGE ( 'NONE', *, *, #140232, .F. ) ;
#111644=VECTOR ( 'NONE', #63926, 999.9999999999998863 ) ;
#111645=ORIENTED_EDGE ( 'NONE', *, *, #24055, .F. ) ;
#111646=ORIENTED_EDGE ( 'NONE', *, *, #108765, .T. ) ;
#111647=VECTOR ( 'NONE', #34031, 1000.000000000000114 ) ;
#111648=EDGE_LOOP ( 'NONE', ( #118784, #4599, #91365, #16045 ) ) ;
#111649=DIRECTION ( 'NONE',  ( -0.000000000000000000, -0.3543493200069152693, 0.9351131265310292928 ) ) ;
#111650=CARTESIAN_POINT ( 'NONE',  ( 19.05000000000000071, 3.174999999999997158, 4.000000000000000000 ) ) ;
#111651=VECTOR ( 'NONE', #54288, 1000.000000000000000 ) ;
#111652=PLANE ( 'NONE',  #119479 ) ;
#111653=VERTEX_POINT ( 'NONE', #30386 ) ;
#111655=CARTESIAN_POINT ( 'NONE',  ( 4.499999999999968914, 22.22500000000000142, 4.362957392718803007 ) ) ;
#111656=PLANE ( 'NONE',  #60327 ) ;
#111657=DIRECTION ( 'NONE',  ( -0.7071067811865486830, 0.7071067811865464625, 0.000000000000000000 ) ) ;
#111658=ORIENTED_EDGE ( 'NONE', *, *, #44779, .T. ) ;
#111659=CARTESIAN_POINT ( 'NONE',  ( -33.18398860626899705, 28.73617430169810305, 5.000000000000000000 ) ) ;
#111660=CARTESIAN_POINT ( 'NONE',  ( -63.29974487139158867, -27.71228299555250274, 4.000000000000000000 ) ) ;
#111661=PLANE ( 'NONE',  #42720 ) ;
#111662=CARTESIAN_POINT ( 'NONE',  ( 34.92499999999998295, 14.81665438641030264, 4.500000000000000888 ) ) ;
#111664=PLANE ( 'NONE',  #9849 ) ;
#111665=LINE ( 'NONE', #56619, #133395 ) ;
#111666=DIRECTION ( 'NONE',  ( 0.7071067811865486830, -0.7071067811865464625, -0.000000000000000000 ) ) ;
#111667=FACE_OUTER_BOUND ( 'NONE', #61625, .T. ) ;
#111669=EDGE_CURVE ( 'NONE', #107040, #114480, #127562, .T. ) ;
#111673=ORIENTED_EDGE ( 'NONE', *, *, #87375, .T. ) ;
#111674=VECTOR ( 'NONE', #78704, 1000.000000000000227 ) ;
#111676=VECTOR ( 'NONE', #107854, 1000.000000000000227 ) ;
#111677=CARTESIAN_POINT ( 'NONE',  ( -2.816011393730999401, 28.73617430169785436, 5.000000000000000000 ) ) ;
#111678=LINE ( 'NONE', #100799, #2676 ) ;
#111681=ORIENTED_EDGE ( 'NONE', *, *, #108494, .T. ) ;
#111683=VECTOR ( 'NONE', #139976, 1000.000000000000114 ) ;
#111684=CARTESIAN_POINT ( 'NONE',  ( -21.48921356237309155, -27.52281430457070499, 5.000000000000000000 ) ) ;
#111685=VECTOR ( 'NONE', #48565, 1000.000000000000227 ) ;
#111686=DIRECTION ( 'NONE',  ( 0.7071067811865487940, -0.7071067811865463515, 0.000000000000000000 ) ) ;
#111687=VERTEX_POINT ( 'NONE', #94907 ) ;
#111688=ORIENTED_EDGE ( 'NONE', *, *, #139362, .T. ) ;
#111691=CARTESIAN_POINT ( 'NONE',  ( -4.499999999999968914, -14.56887692260766265, 4.000000000000000000 ) ) ;
#111694=EDGE_LOOP ( 'NONE', ( #3462, #41680, #40787, #25859 ) ) ;
#111695=LINE ( 'NONE', #120381, #94128 ) ;
#111696=EDGE_LOOP ( 'NONE', ( #121775, #134470, #35224, #13920 ) ) ;
#111697=ORIENTED_EDGE ( 'NONE', *, *, #8166, .T. ) ;
#111699=VECTOR ( 'NONE', #107652, 999.9999999999998863 ) ;
#111700=VERTEX_POINT ( 'NONE', #139890 ) ;
#111701=VECTOR ( 'NONE', #98157, 1000.000000000000000 ) ;
#111705=DIRECTION ( 'NONE',  ( 0.3543493200069162685, -0.000000000000000000, -0.9351131265310288487 ) ) ;
#111706=ORIENTED_EDGE ( 'NONE', *, *, #143283, .T. ) ;
#111707=PLANE ( 'NONE',  #64532 ) ;
#111708=AXIS2_PLACEMENT_3D ( 'NONE', #53922, #41573, #85794 ) ;
#111709=CARTESIAN_POINT ( 'NONE',  ( -53.99451991528749062, 28.92564299267975869, 4.000000000000000000 ) ) ;
#111712=DIRECTION ( 'NONE',  ( -0.000000000000000000, 0.000000000000000000, 1.000000000000000000 ) ) ;
#111713=EDGE_CURVE ( 'NONE', #76630, #137730, #7895, .T. ) ;
#111714=FACE_BOUND ( 'NONE', #67009, .T. ) ;
#111717=EDGE_CURVE ( 'NONE', #1213, #61607, #63749, .T. ) ;
#111718=LINE ( 'NONE', #26137, #53023 ) ;
#111719=EDGE_CURVE ( 'NONE', #85558, #84409, #89070, .T. ) ;
#111720=PLANE ( 'NONE',  #37530 ) ;
#111721=DIRECTION ( 'NONE',  ( 1.000000000000000000, 0.000000000000000000, 0.000000000000000000 ) ) ;
#111722=ORIENTED_EDGE ( 'NONE', *, *, #88658, .F. ) ;
#111724=ORIENTED_EDGE ( 'NONE', *, *, #36798, .F. ) ;
#111725=ORIENTED_EDGE ( 'NONE', *, *, #48801, .T. ) ;
#111726=VERTEX_POINT ( 'NONE', #120952 ) ;
#111727=EDGE_CURVE ( 'NONE', #52145, #40163, #54315, .T. ) ;
#111730=EDGE_LOOP ( 'NONE', ( #122743, #120878, #92206, #90538 ) ) ;
#111731=VECTOR ( 'NONE', #131588, 1000.000000000000000 ) ;
#111733=DIRECTION ( 'NONE',  ( 0.7071067811865487940, -0.7071067811865463515, 0.000000000000000000 ) ) ;
#111734=EDGE_CURVE ( 'NONE', #142281, #68447, #142029, .T. ) ;
#111735=VERTEX_POINT ( 'NONE', #119501 ) ;
#111737=AXIS2_PLACEMENT_3D ( 'NONE', #84811, #18825, #84132 ) ;
#111738=ADVANCED_FACE ( 'NONE', ( #31816 ), #76038, .F. ) ;
#111739=CARTESIAN_POINT ( 'NONE',  ( 0.000000000000000000, 0.000000000000000000, 5.000000000000000000 ) ) ;
#111740=CARTESIAN_POINT ( 'NONE',  ( 25.49999999999982236, 4.466399257802211586, 5.000000000000000000 ) ) ;
#111741=FACE_OUTER_BOUND ( 'NONE', #25200, .T. ) ;
#111742=VECTOR ( 'NONE', #59890, 1000.000000000000000 ) ;
#111743=DIRECTION ( 'NONE',  ( 0.6830127018922181881, 0.6830127018922202975, -0.2588190451025214056 ) ) ;
#111744=ORIENTED_EDGE ( 'NONE', *, *, #31110, .T. ) ;
#111745=EDGE_LOOP ( 'NONE', ( #136726, #90554, #69574, #10687 ) ) ;
#111746=VERTEX_POINT ( 'NONE', #89755 ) ;
#111748=EDGE_LOOP ( 'NONE', ( #39366, #42722, #107101, #111281 ) ) ;
#111750=DIRECTION ( 'NONE',  ( -0.7071067811865486830, 0.7071067811865464625, 0.000000000000000000 ) ) ;
#111751=EDGE_CURVE ( 'NONE', #82218, #13451, #110768, .T. ) ;
#111753=ORIENTED_EDGE ( 'NONE', *, *, #43235, .F. ) ;
#111755=DIRECTION ( 'NONE',  ( -0.7071067811865486830, -0.7071067811865464625, -0.000000000000000000 ) ) ;
#111757=VERTEX_POINT ( 'NONE', #11454 ) ;
#111758=CARTESIAN_POINT ( 'NONE',  ( -1.499999999999987566, -19.53360074219753884, 5.000000000000000000 ) ) ;
#111759=EDGE_CURVE ( 'NONE', #19965, #40586, #111512, .T. ) ;
#111760=CARTESIAN_POINT ( 'NONE',  ( 26.29298673570676215, -21.74070752338406365, 4.999753212805220670 ) ) ;
#111762=CARTESIAN_POINT ( 'NONE',  ( 0.000000000000000000, 0.000000000000000000, 5.000000000000000000 ) ) ;
#111765=LINE ( 'NONE', #46554, #22120 ) ;
#111766=DIRECTION ( 'NONE',  ( 0.000000000000000000, -1.000000000000000000, 0.000000000000000000 ) ) ;
#111767=CARTESIAN_POINT ( 'NONE',  ( -34.45011844616455221, -7.483719188362438324, 5.000000000000000888 ) ) ;
#111768=AXIS2_PLACEMENT_3D ( 'NONE', #57715, #22877, #110610 ) ;
#111769=EDGE_CURVE ( 'NONE', #59176, #60739, #22326, .T. ) ;
#111770=FACE_OUTER_BOUND ( 'NONE', #57408, .T. ) ;
#111771=CARTESIAN_POINT ( 'NONE',  ( 12.18398860626900060, 28.73617430169795739, 5.000000000000000000 ) ) ;
#111772=ORIENTED_EDGE ( 'NONE', *, *, #4654, .F. ) ;
#111773=FACE_OUTER_BOUND ( 'NONE', #45288, .T. ) ;
#111774=AXIS2_PLACEMENT_3D ( 'NONE', #24282, #104687, #103254 ) ;
#111775=ORIENTED_EDGE ( 'NONE', *, *, #19772, .T. ) ;
#111776=FACE_OUTER_BOUND ( 'NONE', #112313, .T. ) ;
#111778=EDGE_CURVE ( 'NONE', #15594, #29105, #100654, .T. ) ;
#111779=LINE ( 'NONE', #113909, #25079 ) ;
#111781=LINE ( 'NONE', #58153, #136741 ) ;
#111782=CARTESIAN_POINT ( 'NONE',  ( 4.771493228613326032, 20.25929247661551003, 7.808871592221780844 ) ) ;
#111783=VERTEX_POINT ( 'NONE', #133291 ) ;
#111785=CARTESIAN_POINT ( 'NONE',  ( -16.49999999999988276, -20.53675388469232033, 2.352720554255855134 ) ) ;
#111788=LINE ( 'NONE', #88621, #117849 ) ;
#111789=DIRECTION ( 'NONE',  ( 0.6830127018922180770, -0.6830127018922204085, -0.2588190451025213501 ) ) ;
#111790=ORIENTED_EDGE ( 'NONE', *, *, #60928, .T. ) ;
#111791=ORIENTED_EDGE ( 'NONE', *, *, #17580, .T. ) ;
#111792=AXIS2_PLACEMENT_3D ( 'NONE', #104318, #128255, #4986 ) ;
#111793=CARTESIAN_POINT ( 'NONE',  ( -13.10530833935383299, 3.713635273109021639, 4.055062020558137803 ) ) ;
#111794=ORIENTED_EDGE ( 'NONE', *, *, #93006, .F. ) ;
#111795=LINE ( 'NONE', #12461, #108502 ) ;
#111797=DIRECTION ( 'NONE',  ( 0.7071067811865486830, -0.7071067811865464625, -0.000000000000000000 ) ) ;
#111798=ORIENTED_EDGE ( 'NONE', *, *, #99841, .T. ) ;
#111799=EDGE_CURVE ( 'NONE', #43144, #62908, #23800, .T. ) ;
#111800=CARTESIAN_POINT ( 'NONE',  ( -31.49999999999977973, -16.53360074219757792, 5.000000000000000000 ) ) ;
#111801=LINE ( 'NONE', #89330, #139337 ) ;
#111803=VECTOR ( 'NONE', #13860, 999.9999999999998863 ) ;
#111804=CARTESIAN_POINT ( 'NONE',  ( 7.499999999999944045, -8.568876922607730151, 4.000000000000000000 ) ) ;
#111805=CARTESIAN_POINT ( 'NONE',  ( -8.999999999999937828, 10.21212019023808004, -2.019456568337778979 ) ) ;
#111807=EDGE_CURVE ( 'NONE', #23719, #115183, #136831, .T. ) ;
#111809=AXIS2_PLACEMENT_3D ( 'NONE', #60270, #71861, #103037 ) ;
#111810=ORIENTED_EDGE ( 'NONE', *, *, #38769, .F. ) ;
#111811=VECTOR ( 'NONE', #22715, 1000.000000000000000 ) ;
#111812=ORIENTED_EDGE ( 'NONE', *, *, #127048, .T. ) ;
#111813=ORIENTED_EDGE ( 'NONE', *, *, #78186, .T. ) ;
#111815=ORIENTED_EDGE ( 'NONE', *, *, #899, .T. ) ;
#111816=ORIENTED_EDGE ( 'NONE', *, *, #105961, .T. ) ;
#111817=ORIENTED_EDGE ( 'NONE', *, *, #108494, .F. ) ;
#111818=VECTOR ( 'NONE', #101756, 1000.000000000000000 ) ;
#111819=VECTOR ( 'NONE', #118598, 1000.000000000000000 ) ;
#111822=CARTESIAN_POINT ( 'NONE',  ( 17.29289321881334018, -12.74070752338414714, 5.000000000000000000 ) ) ;
#111823=EDGE_LOOP ( 'NONE', ( #107476, #39746, #76166, #15622 ) ) ;
#111824=CARTESIAN_POINT ( 'NONE',  ( -17.99999999999986500, 14.58746187583909126, 4.000000000000000000 ) ) ;
#111825=DIRECTION ( 'NONE',  ( -0.000000000000000000, -0.3543493200069152693, 0.9351131265310292928 ) ) ;
#111827=EDGE_CURVE ( 'NONE', #16613, #17766, #14344, .T. ) ;
#111828=CARTESIAN_POINT ( 'NONE',  ( -57.48921356237308800, -27.52281430457095368, 5.000000000000000000 ) ) ;
#111830=EDGE_LOOP ( 'NONE', ( #45101, #63123, #82828, #53798 ) ) ;
#111831=ADVANCED_FACE ( 'NONE', ( #90485 ), #134733, .F. ) ;
#111832=LINE ( 'NONE', #80636, #11750 ) ;
#111833=CARTESIAN_POINT ( 'NONE',  ( 28.78501580275792548, -3.740707523384241728, 15.76143240460130635 ) ) ;
#111834=AXIS2_PLACEMENT_3D ( 'NONE', #108048, #85599, #63886 ) ;
#111835=CARTESIAN_POINT ( 'NONE',  ( -29.16347128873433192, 15.75929247661555443, 9.299976744542854945 ) ) ;
#111836=DIRECTION ( 'NONE',  ( 0.000000000000000000, -0.3543493200069153248, -0.9351131265310291818 ) ) ;
#111837=DIRECTION ( 'NONE',  ( -0.6830127018922180770, -0.6830127018922204085, -0.2588190451025213501 ) ) ;
#111839=DIRECTION ( 'NONE',  ( 0.7071067811865487940, -0.7071067811865463515, 0.000000000000000000 ) ) ;
#111841=CARTESIAN_POINT ( 'NONE',  ( -10.49999999999993250, 7.087461875839178305, 4.000000000000000000 ) ) ;
#111842=VECTOR ( 'NONE', #52245, 1000.000000000000227 ) ;
#111843=CARTESIAN_POINT ( 'NONE',  ( 0.000000000000000000, 0.000000000000000000, 5.000000000000000000 ) ) ;
#111844=ORIENTED_EDGE ( 'NONE', *, *, #105743, .T. ) ;
#111845=ORIENTED_EDGE ( 'NONE', *, *, #31276, .F. ) ;
#111847=LINE ( 'NONE', #77096, #67167 ) ;
#111849=LINE ( 'NONE', #53920, #84944 ) ;
#111850=EDGE_CURVE ( 'NONE', #110456, #39448, #104171, .T. ) ;
#111853=EDGE_CURVE ( 'NONE', #6385, #103176, #34684, .T. ) ;
#111855=VECTOR ( 'NONE', #126382, 1000.000000000000000 ) ;
#111856=ORIENTED_EDGE ( 'NONE', *, *, #104590, .F. ) ;
#111857=DIRECTION ( 'NONE',  ( 0.3543493200069162685, -0.000000000000000000, -0.9351131265310288487 ) ) ;
#111858=ORIENTED_EDGE ( 'NONE', *, *, #142705, .F. ) ;
#111859=ORIENTED_EDGE ( 'NONE', *, *, #18728, .T. ) ;
#111860=CARTESIAN_POINT ( 'NONE',  ( -34.92500000000001137, -4.662012949885770752, -5.188494296035321973 ) ) ;
#111861=DIRECTION ( 'NONE',  ( 0.3543493200069163240, 0.000000000000000000, 0.9351131265310288487 ) ) ;
#111862=CARTESIAN_POINT ( 'NONE',  ( 48.18398860626899705, 28.73617430169820608, 5.000000000000000000 ) ) ;
#111863=ORIENTED_EDGE ( 'NONE', *, *, #138540, .F. ) ;
#111864=ADVANCED_FACE ( 'NONE', ( #57173 ), #69466, .F. ) ;
#111865=CARTESIAN_POINT ( 'NONE',  ( 5.510786437626906675, -27.52281430457051314, 5.000000000000000000 ) ) ;
#111866=ORIENTED_EDGE ( 'NONE', *, *, #48641, .T. ) ;
#111868=CARTESIAN_POINT ( 'NONE',  ( -23.67183060077630685, -3.740707523384246613, 4.000000000000000000 ) ) ;
#111869=LINE ( 'NONE', #133622, #96286 ) ;
#111870=DIRECTION ( 'NONE',  ( -0.6830127018922180770, -0.6830127018922204085, -0.2588190451025213501 ) ) ;
#111871=CARTESIAN_POINT ( 'NONE',  ( -14.29298673570684919, -21.74070752338405299, 4.999753212805220670 ) ) ;
#111872=VECTOR ( 'NONE', #139984, 1000.000000000000000 ) ;
#111875=CARTESIAN_POINT ( 'NONE',  ( 51.18398860626899705, 28.73617430169823095, 5.000000000000000000 ) ) ;
#111877=PLANE ( 'NONE',  #129815 ) ;
#111878=PLANE ( 'NONE',  #61679 ) ;
#111879=DIRECTION ( 'NONE',  ( 0.7071067811865486830, -0.7071067811865464625, -0.000000000000000000 ) ) ;
#111880=ORIENTED_EDGE ( 'NONE', *, *, #12751, .T. ) ;
#111881=PLANE ( 'NONE',  #603 ) ;
#111885=ORIENTED_EDGE ( 'NONE', *, *, #100917, .F. ) ;
#111886=PLANE ( 'NONE',  #9863 ) ;
#111887=DIRECTION ( 'NONE',  ( 1.000000000000000000, 0.000000000000000000, 0.000000000000000000 ) ) ;
#111889=LINE ( 'NONE', #24160, #136535 ) ;
#111890=VECTOR ( 'NONE', #91718, 1000.000000000000000 ) ;
#111892=CARTESIAN_POINT ( 'NONE',  ( -15.48921356237309510, -27.52281430457066236, 5.000000000000000000 ) ) ;
#111893=FACE_BOUND ( 'NONE', #46281, .T. ) ;
#111894=CARTESIAN_POINT ( 'NONE',  ( 34.17183060077623225, 18.75929247661552068, 4.000000000000000000 ) ) ;
#111896=EDGE_CURVE ( 'NONE', #131061, #66262, #71593, .T. ) ;
#111897=PLANE ( 'NONE',  #44475 ) ;
#111898=VECTOR ( 'NONE', #20001, 999.9999999999998863 ) ;
#111899=FACE_OUTER_BOUND ( 'NONE', #130133, .T. ) ;
#111900=LINE ( 'NONE', #56841, #13392 ) ;
#111901=ORIENTED_EDGE ( 'NONE', *, *, #81250, .T. ) ;
#111902=FACE_OUTER_BOUND ( 'NONE', #92627, .T. ) ;
#111903=ORIENTED_EDGE ( 'NONE', *, *, #131913, .F. ) ;
#111904=ADVANCED_FACE ( 'NONE', ( #72345 ), #115755, .F. ) ;
#111906=VERTEX_POINT ( 'NONE', #84610 ) ;
#111910=EDGE_CURVE ( 'NONE', #81140, #59816, #127379, .T. ) ;
#111911=DIRECTION ( 'NONE',  ( 0.7071067811865486830, -0.7071067811865464625, -0.000000000000000000 ) ) ;
#111912=ADVANCED_FACE ( 'NONE', ( #105604 ), #7727, .T. ) ;
#111913=ORIENTED_EDGE ( 'NONE', *, *, #77217, .F. ) ;
#111914=CARTESIAN_POINT ( 'NONE',  ( 0.000000000000000000, 0.000000000000000000, 5.000000000000000000 ) ) ;
#111915=CIRCLE ( 'NONE', #130440, 0.5000000000000000000 ) ;
#111917=VECTOR ( 'NONE', #2959, 1000.000000000000000 ) ;
#111918=LINE ( 'NONE', #22025, #98201 ) ;
#111919=EDGE_CURVE ( 'NONE', #142250, #28108, #19341, .T. ) ;
#111920=CARTESIAN_POINT ( 'NONE',  ( -34.49999999999976552, -8.945670655168967755, 4.994342998332164996 ) ) ;
#111922=CARTESIAN_POINT ( 'NONE',  ( -24.99581563014004715, 3.703558271726549833, 4.317415941188012418 ) ) ;
#111923=CARTESIAN_POINT ( 'NONE',  ( -28.49999999999979750, -11.56887692260769640, 4.000000000000000000 ) ) ;
#111924=FACE_OUTER_BOUND ( 'NONE', #112875, .T. ) ;
#111925=LINE ( 'NONE', #36492, #76340 ) ;
#111926=ORIENTED_EDGE ( 'NONE', *, *, #98195, .F. ) ;
#111927=AXIS2_PLACEMENT_3D ( 'NONE', #108396, #95421, #84571 ) ;
#111929=ORIENTED_EDGE ( 'NONE', *, *, #46698, .T. ) ;
#111931=LINE ( 'NONE', #56868, #139260 ) ;
#111932=EDGE_LOOP ( 'NONE', ( #70770, #53945, #1159, #50397 ) ) ;
#111933=EDGE_CURVE ( 'NONE', #49793, #78390, #28805, .T. ) ;
#111934=EDGE_LOOP ( 'NONE', ( #60573, #25017, #141661, #76276 ) ) ;
#111935=EDGE_LOOP ( 'NONE', ( #22275, #6622, #72956, #104893 ) ) ;
#111936=CARTESIAN_POINT ( 'NONE',  ( 0.000000000000000000, 0.000000000000000000, 5.000000000000000000 ) ) ;
#111937=ORIENTED_EDGE ( 'NONE', *, *, #110326, .T. ) ;
#111938=FACE_OUTER_BOUND ( 'NONE', #59198, .T. ) ;
#111939=AXIS2_PLACEMENT_3D ( 'NONE', #80018, #24874, #82152 ) ;
#111940=EDGE_CURVE ( 'NONE', #79668, #27936, #30208, .T. ) ;
#111942=AXIS2_PLACEMENT_3D ( 'NONE', #47840, #134842, #80449 ) ;
#111945=ORIENTED_EDGE ( 'NONE', *, *, #114974, .T. ) ;
#111946=CARTESIAN_POINT ( 'NONE',  ( -5.816011393731002066, 28.73617430169783304, 5.000000000000000000 ) ) ;
#111947=CARTESIAN_POINT ( 'NONE',  ( 30.48921356237309510, -27.52281430457076894, 5.000000000000000000 ) ) ;
#111948=DIRECTION ( 'NONE',  ( 0.3543493200069162685, -0.000000000000000000, -0.9351131265310288487 ) ) ;
#111949=DIRECTION ( 'NONE',  ( 0.6830127018922181881, 0.6830127018922202975, -0.2588190451025214056 ) ) ;
#111950=VERTEX_POINT ( 'NONE', #106310 ) ;
#111953=DIRECTION ( 'NONE',  ( -0.7071067811865487940, 0.7071067811865463515, -0.000000000000000000 ) ) ;
#111954=AXIS2_PLACEMENT_3D ( 'NONE', #27218, #104790, #96045 ) ;
#111955=FACE_OUTER_BOUND ( 'NONE', #95126, .T. ) ;
#111956=ORIENTED_EDGE ( 'NONE', *, *, #50956, .F. ) ;
#111957=DIRECTION ( 'NONE',  ( 1.000000000000000000, 0.000000000000000000, 0.000000000000000000 ) ) ;
#111958=EDGE_CURVE ( 'NONE', #15581, #39740, #74457, .T. ) ;
#111959=DIRECTION ( 'NONE',  ( 0.7071067811865487940, -0.7071067811865463515, 0.000000000000000000 ) ) ;
#111962=EDGE_CURVE ( 'NONE', #70329, #45800, #120780, .T. ) ;
#111963=DIRECTION ( 'NONE',  ( 0.3543493200069162685, -0.000000000000000000, -0.9351131265310288487 ) ) ;
#111964=CARTESIAN_POINT ( 'NONE',  ( 0.4892135623730947680, -27.52281430457055578, 5.000000000000000000 ) ) ;
#111965=CARTESIAN_POINT ( 'NONE',  ( 5.999999999999956479, 13.93112307739204425, 4.000000000000000000 ) ) ;
#111967=CARTESIAN_POINT ( 'NONE',  ( -48.29974487139158867, -27.71228299555239971, 4.000000000000000000 ) ) ;
#111968=EDGE_CURVE ( 'NONE', #93963, #95860, #88906, .T. ) ;
#111969=CARTESIAN_POINT ( 'NONE',  ( -20.20710678118641113, -17.24070752338409918, 5.000000000000000000 ) ) ;
#111971=DIRECTION ( 'NONE',  ( 0.7071067811865486830, -0.7071067811865464625, -0.000000000000000000 ) ) ;
#111972=CARTESIAN_POINT ( 'NONE',  ( 18.85005128541013164, -8.240707523384189770, 17.25253755692243374 ) ) ;
#111974=EDGE_LOOP ( 'NONE', ( #76018, #5702, #49590, #33886 ) ) ;
#111975=CARTESIAN_POINT ( 'NONE',  ( 19.49999999999986144, -17.56887692260763956, 4.000000000000000000 ) ) ;
#111976=CARTESIAN_POINT ( 'NONE',  ( -28.01987774928530683, -17.24070752338410983, 20.23474786156463168 ) ) ;
#111977=VECTOR ( 'NONE', #68592, 1000.000000000000000 ) ;
#111978=CARTESIAN_POINT ( 'NONE',  ( 24.32816939922335919, -0.7407075233842735917, 4.000000000000000000 ) ) ;
#111979=DIRECTION ( 'NONE',  ( 0.000000000000000000, -0.3543493200069153248, -0.9351131265310291818 ) ) ;
#111981=EDGE_LOOP ( 'NONE', ( #66287, #69216, #9650 ) ) ;
#111982=CARTESIAN_POINT ( 'NONE',  ( -42.48921356237308800, -27.52281430457085065, 5.000000000000000000 ) ) ;
#111983=( BOUNDED_CURVE ( )  B_SPLINE_CURVE ( 3, ( #135365, #36048, #14266, #88997 ),
 .UNSPECIFIED., .F., .T. ) 
 B_SPLINE_CURVE_WITH_KNOTS ( ( 4, 4 ),
 ( 5.005968288816726286, 5.074607125596334534 ),
 .UNSPECIFIED. ) 
 CURVE ( )  GEOMETRIC_REPRESENTATION_ITEM ( )  RATIONAL_B_SPLINE_CURVE ( ( 1.000000000000000000, 0.9996074310407765395, 0.9996074310407765395, 1.000000000000000000 ) ) 
 REPRESENTATION_ITEM ( '' )  );
#111984=CARTESIAN_POINT ( 'NONE',  ( 11.99451991528749417, 28.92564299267946382, 4.000000000000000000 ) ) ;
#111985=VERTEX_POINT ( 'NONE', #20030 ) ;
#111986=ADVANCED_FACE ( 'NONE', ( #130977 ), #143257, .T. ) ;
#111987=CARTESIAN_POINT ( 'NONE',  ( -8.510786437626906675, -27.52281430457049183, 5.000000000000000000 ) ) ;
#111988=CARTESIAN_POINT ( 'NONE',  ( 6.183988606268994381, 28.73617430169791476, 5.000000000000000000 ) ) ;
#111989=CARTESIAN_POINT ( 'NONE',  ( 2.293876922608031332, 22.22500000000000142, 4.000000000000000000 ) ) ;
#111995=LINE ( 'NONE', #115314, #72001 ) ;
#111996=EDGE_CURVE ( 'NONE', #79129, #131121, #99747, .T. ) ;
#111997=EDGE_LOOP ( 'NONE', ( #98282, #110192, #43414, #129882 ) ) ;
#111998=PLANE ( 'NONE',  #65086 ) ;
#112001=DIRECTION ( 'NONE',  ( -0.7071067811865486830, -0.7071067811865464625, -0.000000000000000000 ) ) ;
#112002=DIRECTION ( 'NONE',  ( -0.7071067811865486830, 0.7071067811865464625, 0.000000000000000000 ) ) ;
#112003=LINE ( 'NONE', #80800, #18764 ) ;
#112005=ADVANCED_FACE ( 'NONE', ( #86026 ), #64276, .F. ) ;
#112006=LINE ( 'NONE', #56924, #74242 ) ;
#112007=CARTESIAN_POINT ( 'NONE',  ( -0.1839886062690032631, 28.73617430169787568, 5.000000000000000000 ) ) ;
#112008=VERTEX_POINT ( 'NONE', #41811 ) ;
#112010=ORIENTED_EDGE ( 'NONE', *, *, #16544, .F. ) ;
#112011=CARTESIAN_POINT ( 'NONE',  ( 34.92499999999998295, 22.22500000000000142, 4.500000000000000888 ) ) ;
#112013=CARTESIAN_POINT ( 'NONE',  ( 32.99451991528749062, 28.92564299267960948, 4.000000000000000000 ) ) ;
#112014=CARTESIAN_POINT ( 'NONE',  ( -47.99451991528749062, 28.92564299267971251, 4.000000000000000000 ) ) ;
#112016=DIRECTION ( 'NONE',  ( -0.6830127018922180770, -0.6830127018922204085, -0.2588190451025213501 ) ) ;
#112017=VECTOR ( 'NONE', #61497, 999.9999999999998863 ) ;
#112018=CARTESIAN_POINT ( 'NONE',  ( -7.171830600776425868, -8.240707523384207533, 4.000000000000000000 ) ) ;
#112022=DIRECTION ( 'NONE',  ( -0.7071067811865486830, -0.7071067811865464625, 0.000000000000000000 ) ) ;
#112023=LINE ( 'NONE', #76547, #121466 ) ;
#112024=ORIENTED_EDGE ( 'NONE', *, *, #41035, .F. ) ;
#112027=DIRECTION ( 'NONE',  ( -0.3543493200069162685, -0.000000000000000000, -0.9351131265310288487 ) ) ;
#112028=EDGE_CURVE ( 'NONE', #44279, #52361, #67136, .T. ) ;
#112031=ORIENTED_EDGE ( 'NONE', *, *, #61401, .F. ) ;
#112032=ORIENTED_EDGE ( 'NONE', *, *, #35864, .T. ) ;
#112033=DIRECTION ( 'NONE',  ( 0.7071067811865487940, 0.7071067811865463515, 0.000000000000000000 ) ) ;
#112036=EDGE_CURVE ( 'NONE', #57693, #89225, #88177, .T. ) ;
#112037=PLANE ( 'NONE',  #122928 ) ;
#112038=LINE ( 'NONE', #67852, #5915 ) ;
#112039=VERTEX_POINT ( 'NONE', #414 ) ;
#112041=CARTESIAN_POINT ( 'NONE',  ( -7.171830600776411657, 6.759292476615649470, 4.000000000000000000 ) ) ;
#112042=CARTESIAN_POINT ( 'NONE',  ( 3.183988606268992161, 28.73617430169789699, 5.000000000000000000 ) ) ;
#112043=VECTOR ( 'NONE', #133841, 1000.000000000000000 ) ;
#112044=ORIENTED_EDGE ( 'NONE', *, *, #45338, .T. ) ;
#112045=VERTEX_POINT ( 'NONE', #130265 ) ;
#112047=VECTOR ( 'NONE', #132895, 1000.000000000000000 ) ;
#112048=ORIENTED_EDGE ( 'NONE', *, *, #85641, .T. ) ;
#112049=DIRECTION ( 'NONE',  ( 1.000000000000000000, 0.000000000000000000, 0.000000000000000000 ) ) ;
#112050=CARTESIAN_POINT ( 'NONE',  ( 12.29974487139158512, -27.71228299555214747, 4.000000000000000000 ) ) ;
#112052=CARTESIAN_POINT ( 'NONE',  ( 0.000000000000000000, 0.000000000000000000, 5.000000000000000000 ) ) ;
#112053=CARTESIAN_POINT ( 'NONE',  ( -33.79333936457824450, 21.75929247661549581, 4.998822639870701856 ) ) ;
#112056=CARTESIAN_POINT ( 'NONE',  ( -17.70822291016941463, -15.74070752338411694, 19.73771281079093143 ) ) ;
#112058=VECTOR ( 'NONE', #45817, 999.9999999999998863 ) ;
#112059=VERTEX_POINT ( 'NONE', #132430 ) ;
#112060=VECTOR ( 'NONE', #55257, 1000.000000000000227 ) ;
#112061=DIRECTION ( 'NONE',  ( -0.3543493200069162685, -0.000000000000000000, -0.9351131265310288487 ) ) ;
#112062=EDGE_CURVE ( 'NONE', #16561, #59489, #33119, .T. ) ;
#112064=DIRECTION ( 'NONE',  ( 0.6830127018922181881, 0.6830127018922202975, -0.2588190451025214056 ) ) ;
#112065=EDGE_LOOP ( 'NONE', ( #121720, #12437, #72510, #40154 ) ) ;
#112066=AXIS2_PLACEMENT_3D ( 'NONE', #28269, #72530, #17375 ) ;
#112067=STYLED_ITEM ( 'NONE', ( #125505 ), #45918 ) ;
#112068=FACE_BOUND ( 'NONE', #38840, .T. ) ;
#112069=CARTESIAN_POINT ( 'NONE',  ( -15.88837638105231775, 9.759292476615614831, 17.35367589129216270 ) ) ;
#112070=CARTESIAN_POINT ( 'NONE',  ( 3.489213562373097322, -27.52281430457057709, 5.000000000000000000 ) ) ;
#112072=LINE ( 'NONE', #46114, #45743 ) ;
#112073=VECTOR ( 'NONE', #132632, 1000.000000000000000 ) ;
#112074=LINE ( 'NONE', #22870, #7202 ) ;
#112076=VERTEX_POINT ( 'NONE', #44715 ) ;
#112077=EDGE_CURVE ( 'NONE', #108713, #9196, #32365, .T. ) ;
#112078=ORIENTED_EDGE ( 'NONE', *, *, #50710, .F. ) ;
#112080=ORIENTED_EDGE ( 'NONE', *, *, #4499, .F. ) ;
#112082=CARTESIAN_POINT ( 'NONE',  ( -23.99451991528749062, 28.92564299267954908, 4.000000000000000000 ) ) ;
#112084=EDGE_CURVE ( 'NONE', #128697, #103370, #77329, .T. ) ;
#112086=LINE ( 'NONE', #101184, #16875 ) ;
#112087=EDGE_CURVE ( 'NONE', #140745, #114242, #14877, .T. ) ;
#112088=PLANE ( 'NONE',  #43239 ) ;
#112089=VECTOR ( 'NONE', #31498, 1000.000000000000227 ) ;
#112090=LINE ( 'NONE', #1142, #81887 ) ;
#112092=CARTESIAN_POINT ( 'NONE',  ( -4.499999999999968914, 13.08746187583912146, 4.000000000000000000 ) ) ;
#112095=ADVANCED_FACE ( 'NONE', ( #79487 ), #48226, .T. ) ;
#112098=CARTESIAN_POINT ( 'NONE',  ( 34.42499999999998295, 11.97718569542927014, 5.000000000000000000 ) ) ;
#112099=CARTESIAN_POINT ( 'NONE',  ( 27.81246187583927565, -22.22500000000000142, 4.000000000000000000 ) ) ;
#112102=ORIENTED_EDGE ( 'NONE', *, *, #132480, .F. ) ;
#112105=EDGE_CURVE ( 'NONE', #120482, #39654, #90295, .T. ) ;
#112106=ORIENTED_EDGE ( 'NONE', *, *, #55511, .T. ) ;
#112107=VERTEX_POINT ( 'NONE', #135270 ) ;
#112108=EDGE_CURVE ( 'NONE', #46507, #118828, #56300, .T. ) ;
#112109=ORIENTED_EDGE ( 'NONE', *, *, #137310, .T. ) ;
#112111=EDGE_LOOP ( 'NONE', ( #49374, #70085, #59591, #19518 ) ) ;
#112112=ADVANCED_FACE ( 'NONE', ( #100482 ), #3277, .F. ) ;
#112116=CARTESIAN_POINT ( 'NONE',  ( -34.49999999999975131, 19.46425560840030400, 4.994342998332171213 ) ) ;
#112117=EDGE_LOOP ( 'NONE', ( #6405, #30735, #90881, #59031 ) ) ;
#112119=PLANE ( 'NONE',  #108889 ) ;
#112121=VERTEX_POINT ( 'NONE', #37362 ) ;
#112124=DIRECTION ( 'NONE',  ( 0.6830127018922181881, 0.6830127018922202975, -0.2588190451025214056 ) ) ;
#112125=CARTESIAN_POINT ( 'NONE',  ( 3.005480084712505828, 28.92564299267936079, 4.000000000000000000 ) ) ;
#112126=ORIENTED_EDGE ( 'NONE', *, *, #108525, .F. ) ;
#112127=DIRECTION ( 'NONE',  ( -0.3543493200069162685, -0.000000000000000000, -0.9351131265310288487 ) ) ;
#112128=ORIENTED_EDGE ( 'NONE', *, *, #109148, .F. ) ;
#112129=ORIENTED_EDGE ( 'NONE', *, *, #121194, .F. ) ;
#112130=ORIENTED_EDGE ( 'NONE', *, *, #108416, .F. ) ;
#112131=EDGE_CURVE ( 'NONE', #137290, #86612, #112072, .T. ) ;
#112132=DIRECTION ( 'NONE',  ( -0.7071067811865486830, -0.7071067811865464625, 0.000000000000000000 ) ) ;
#112133=CARTESIAN_POINT ( 'NONE',  ( -15.29974487139158867, -27.71228299555216879, 4.000000000000000000 ) ) ;
#112134=CARTESIAN_POINT ( 'NONE',  ( -26.70822291016936134, -15.74070752338412404, 19.73771281079091366 ) ) ;
#112137=LINE ( 'NONE', #12786, #48879 ) ;
#112138=ORIENTED_EDGE ( 'NONE', *, *, #59166, .F. ) ;
#112139=AXIS2_PLACEMENT_3D ( 'NONE', #11675, #34190, #109594 ) ;
#112140=DIRECTION ( 'NONE',  ( -0.7071067811865486830, 0.7071067811865464625, 0.000000000000000000 ) ) ;
#112141=EDGE_CURVE ( 'NONE', #21912, #50218, #47567, .T. ) ;
#112145=CARTESIAN_POINT ( 'NONE',  ( 13.49999999999990763, -20.56887692260759337, 4.000000000000000000 ) ) ;
#112146=LINE ( 'NONE', #36023, #81418 ) ;
#112147=ORIENTED_EDGE ( 'NONE', *, *, #99933, .F. ) ;
#112148=VECTOR ( 'NONE', #4771, 1000.000000000000000 ) ;
#112149=VERTEX_POINT ( 'NONE', #81598 ) ;
#112150=ADVANCED_FACE ( 'NONE', ( #26478 ), #12013, .F. ) ;
#112151=ORIENTED_EDGE ( 'NONE', *, *, #105519, .T. ) ;
#112152=CARTESIAN_POINT ( 'NONE',  ( -10.49999999999991651, 4.087461875839196956, 4.000000000000000000 ) ) ;
#112153=DIRECTION ( 'NONE',  ( 0.7071067811865486830, -0.7071067811865464625, -0.000000000000000000 ) ) ;
#112154=DIRECTION ( 'NONE',  ( 0.7071067811865487940, 0.7071067811865463515, -0.000000000000000000 ) ) ;
#112155=DIRECTION ( 'NONE',  ( 0.000000000000000000, 1.000000000000000000, 0.000000000000000000 ) ) ;
#112157=CARTESIAN_POINT ( 'NONE',  ( -18.18398860626898994, 28.73617430169800002, 5.000000000000000000 ) ) ;
#112158=VECTOR ( 'NONE', #40481, 999.9999999999998863 ) ;
#112161=CARTESIAN_POINT ( 'NONE',  ( 30.48921356237309510, -27.52281430457076894, 5.000000000000000000 ) ) ;
#112162=CARTESIAN_POINT ( 'NONE',  ( -16.36246187583889622, 22.22500000000000853, 4.000000000000000000 ) ) ;
#112163=ORIENTED_EDGE ( 'NONE', *, *, #29195, .F. ) ;
#112164=CARTESIAN_POINT ( 'NONE',  ( -30.32816939922331656, -9.740707523384182664, 4.000000000000000000 ) ) ;
#112165=EDGE_LOOP ( 'NONE', ( #6802, #140409, #107884, #16514 ) ) ;
#112169=CARTESIAN_POINT ( 'NONE',  ( -19.05000000000000071, 3.174999999999997158, 4.000000000000000000 ) ) ;
#112170=ORIENTED_EDGE ( 'NONE', *, *, #39835, .T. ) ;
#112172=EDGE_CURVE ( 'NONE', #134224, #77753, #101170, .T. ) ;
#112174=DIRECTION ( 'NONE',  ( 1.000000000000000000, 0.000000000000000000, 0.000000000000000000 ) ) ;
#112175=ORIENTED_EDGE ( 'NONE', *, *, #105470, .T. ) ;
#112176=FACE_OUTER_BOUND ( 'NONE', #24792, .T. ) ;
#112177=EDGE_LOOP ( 'NONE', ( #111658, #5415, #140876, #44919 ) ) ;
#112178=DIRECTION ( 'NONE',  ( 0.7071067811865486830, -0.7071067811865464625, -0.000000000000000000 ) ) ;
#112179=EDGE_LOOP ( 'NONE', ( #143548, #15197, #23858, #23898 ) ) ;
#112180=VECTOR ( 'NONE', #28835, 1000.000000000000000 ) ;
#112181=DIRECTION ( 'NONE',  ( 0.3543493200069162685, -0.000000000000000000, -0.9351131265310288487 ) ) ;
#112186=ORIENTED_EDGE ( 'NONE', *, *, #82166, .T. ) ;
#112188=CARTESIAN_POINT ( 'NONE',  ( 4.499999999999968914, -16.53360074219757081, 5.000000000000000000 ) ) ;
#112189=FACE_OUTER_BOUND ( 'NONE', #15379, .T. ) ;
#112191=PLANE ( 'NONE',  #46861 ) ;
#112193=CARTESIAN_POINT ( 'NONE',  ( 12.00548008471251293, 28.92564299267929684, 4.000000000000000000 ) ) ;
#112195=ORIENTED_EDGE ( 'NONE', *, *, #20898, .F. ) ;
#112196=DIRECTION ( 'NONE',  ( 0.7071067811865486830, -0.7071067811865464625, -0.000000000000000000 ) ) ;
#112197=EDGE_LOOP ( 'NONE', ( #23385, #101814, #57046, #113341 ) ) ;
#112198=EDGE_CURVE ( 'NONE', #123070, #101563, #35244, .T. ) ;
#112200=CARTESIAN_POINT ( 'NONE',  ( 0.000000000000000000, 0.000000000000000000, 5.000000000000000000 ) ) ;
#112201=PLANE ( 'NONE',  #33111 ) ;
#112206=EDGE_CURVE ( 'NONE', #131140, #90151, #123679, .T. ) ;
#112207=ORIENTED_EDGE ( 'NONE', *, *, #36894, .F. ) ;
#112209=EDGE_CURVE ( 'NONE', #29743, #77065, #125070, .T. ) ;
#112210=CARTESIAN_POINT ( 'NONE',  ( 39.18398860626899705, 28.73617430169814568, 5.000000000000000000 ) ) ;
#112212=ORIENTED_EDGE ( 'NONE', *, *, #93613, .F. ) ;
#112213=DIRECTION ( 'NONE',  ( -0.7071067811865487940, 0.7071067811865463515, 0.000000000000000000 ) ) ;
#112214=FACE_OUTER_BOUND ( 'NONE', #142701, .T. ) ;
#112216=DIRECTION ( 'NONE',  ( 0.6830127018922180770, -0.6830127018922204085, -0.2588190451025213501 ) ) ;
#112217=VERTEX_POINT ( 'NONE', #57706 ) ;
#112218=ORIENTED_EDGE ( 'NONE', *, *, #137302, .F. ) ;
#112219=ORIENTED_EDGE ( 'NONE', *, *, #89012, .F. ) ;
#112221=ORIENTED_EDGE ( 'NONE', *, *, #133227, .T. ) ;
#112222=PLANE ( 'NONE',  #92593 ) ;
#112223=CARTESIAN_POINT ( 'NONE',  ( -12.32816939922344268, 20.25929247661551713, 4.000000000000000000 ) ) ;
#112224=PLANE ( 'NONE',  #133694 ) ;
#112226=ORIENTED_EDGE ( 'NONE', *, *, #22857, .F. ) ;
#112228=CARTESIAN_POINT ( 'NONE',  ( -11.99999999999992006, 8.587461875839165870, 4.000000000000000000 ) ) ;
#112229=DIRECTION ( 'NONE',  ( 0.7071067811865487940, 0.7071067811865463515, -0.000000000000000000 ) ) ;
#112231=CARTESIAN_POINT ( 'NONE',  ( -5.816011393731002066, 28.73617430169783304, 5.000000000000000000 ) ) ;
#112233=EDGE_LOOP ( 'NONE', ( #112774, #98188, #37344, #21541 ) ) ;
#112234=CARTESIAN_POINT ( 'NONE',  ( -44.99451991528749772, 28.92564299267969474, 4.000000000000000000 ) ) ;
#112235=DIRECTION ( 'NONE',  ( -0.7071067811865487940, 0.7071067811865463515, 0.000000000000000000 ) ) ;
#112236=ORIENTED_EDGE ( 'NONE', *, *, #80541, .F. ) ;
#112237=ORIENTED_EDGE ( 'NONE', *, *, #110295, .F. ) ;
#112241=CARTESIAN_POINT ( 'NONE',  ( -5.671830600776431197, -0.7407075233842770334, 4.000000000000000000 ) ) ;
#112242=LINE ( 'NONE', #58630, #60344 ) ;
#112244=VECTOR ( 'NONE', #105224, 1000.000000000000000 ) ;
#112245=EDGE_CURVE ( 'NONE', #46125, #32348, #61977, .T. ) ;
#112246=ORIENTED_EDGE ( 'NONE', *, *, #21487, .F. ) ;
#112247=ORIENTED_EDGE ( 'NONE', *, *, #19814, .T. ) ;
#112248=EDGE_CURVE ( 'NONE', #97043, #93479, #95293, .T. ) ;
#112251=ORIENTED_EDGE ( 'NONE', *, *, #94425, .F. ) ;
#112252=ORIENTED_EDGE ( 'NONE', *, *, #128583, .F. ) ;
#112254=ADVANCED_FACE ( 'NONE', ( #29318 ), #82304, .F. ) ;
#112255=( BOUNDED_CURVE ( )  B_SPLINE_CURVE ( 3, ( #17171, #49827, #93299, #94699 ),
 .UNSPECIFIED., .F., .F. ) 
 B_SPLINE_CURVE_WITH_KNOTS ( ( 4, 4 ),
 ( 4.767201131347619025, 4.812229608965456151 ),
 .UNSPECIFIED. ) 
 CURVE ( )  GEOMETRIC_REPRESENTATION_ITEM ( )  RATIONAL_B_SPLINE_CURVE ( ( 1.000000000000000000, 0.9998310434873430852, 0.9998310434873430852, 1.000000000000000000 ) ) 
 REPRESENTATION_ITEM ( '' )  );
#112256=CARTESIAN_POINT ( 'NONE',  ( 51.18398860626899705, 28.73617430169823095, 5.000000000000000000 ) ) ;
#112257=ORIENTED_EDGE ( 'NONE', *, *, #1682, .F. ) ;
#112259=LINE ( 'NONE', #111526, #50559 ) ;
#112260=CARTESIAN_POINT ( 'NONE',  ( 34.92499999999998295, -21.72500000000000142, 4.500000000000000888 ) ) ;
#112262=( BOUNDED_CURVE ( )  B_SPLINE_CURVE ( 3, ( #24134, #66927, #35033, #13224 ),
 .UNSPECIFIED., .F., .T. ) 
 B_SPLINE_CURVE_WITH_KNOTS ( ( 4, 4 ),
 ( 3.101920907804234684, 3.199716232068803734 ),
 .UNSPECIFIED. ) 
 CURVE ( )  GEOMETRIC_REPRESENTATION_ITEM ( )  RATIONAL_B_SPLINE_CURVE ( ( 1.000000000000000000, 0.9992031649997841214, 0.9992031649997841214, 1.000000000000000000 ) ) 
 REPRESENTATION_ITEM ( '' )  );
#112263=CARTESIAN_POINT ( 'NONE',  ( -6.299744871391586898, -27.71228299555210484, 4.000000000000000000 ) ) ;
#112265=DIRECTION ( 'NONE',  ( 0.3543493200069163240, 0.000000000000000000, -0.9351131265310288487 ) ) ;
#112266=EDGE_CURVE ( 'NONE', #68252, #64405, #27176, .T. ) ;
#112269=ORIENTED_EDGE ( 'NONE', *, *, #76253, .F. ) ;
#112270=DIRECTION ( 'NONE',  ( -0.3543493200069162685, -0.000000000000000000, -0.9351131265310288487 ) ) ;
#112271=EDGE_CURVE ( 'NONE', #82619, #42670, #71421, .T. ) ;
#112272=EDGE_LOOP ( 'NONE', ( #56970, #59454 ) ) ;
#112273=DIRECTION ( 'NONE',  ( 1.000000000000000000, 0.000000000000000000, 0.000000000000000000 ) ) ;
#112276=ORIENTED_EDGE ( 'NONE', *, *, #122617, .F. ) ;
#112277=EDGE_CURVE ( 'NONE', #88210, #120409, #83748, .T. ) ;
#112278=AXIS2_PLACEMENT_3D ( 'NONE', #142857, #43544, #54450 ) ;
#112280=VECTOR ( 'NONE', #137264, 1000.000000000000000 ) ;
#112281=VECTOR ( 'NONE', #129842, 1000.000000000000227 ) ;
#112282=CARTESIAN_POINT ( 'NONE',  ( 25.49999999999982947, -4.912538124160710673, 4.000000000000000000 ) ) ;
#112283=CARTESIAN_POINT ( 'NONE',  ( 14.99451991528749595, 28.92564299267948513, 4.000000000000000000 ) ) ;
#112285=LINE ( 'NONE', #134771, #17309 ) ;
#112287=CARTESIAN_POINT ( 'NONE',  ( 14.92733143757284786, -1.141545485034857643, 4.000000000000000000 ) ) ;
#112288=FACE_OUTER_BOUND ( 'NONE', #49907, .T. ) ;
#112290=CARTESIAN_POINT ( 'NONE',  ( -17.20666063542140378, 21.75929247661549937, 4.998822639870711626 ) ) ;
#112292=EDGE_LOOP ( 'NONE', ( #54082, #86779, #138857 ) ) ;
#112293=CARTESIAN_POINT ( 'NONE',  ( -24.48921356237309510, -27.52281430457072631, 5.000000000000000000 ) ) ;
#112294=CARTESIAN_POINT ( 'NONE',  ( -13.82816939922344091, 12.75929247661558641, 4.000000000000000000 ) ) ;
#112295=LINE ( 'NONE', #79709, #56489 ) ;
#112296=ORIENTED_EDGE ( 'NONE', *, *, #13510, .F. ) ;
#112297=ORIENTED_EDGE ( 'NONE', *, *, #129943, .F. ) ;
#112299=FACE_OUTER_BOUND ( 'NONE', #85505, .T. ) ;
#112300=ORIENTED_EDGE ( 'NONE', *, *, #12806, .T. ) ;
#112301=LINE ( 'NONE', #655, #39855 ) ;
#112303=CARTESIAN_POINT ( 'NONE',  ( 18.63311396761903538, -2.779424156541560276, 4.000000000000000000 ) ) ;
#112305=CARTESIAN_POINT ( 'NONE',  ( -22.46236777640751114, 22.22500000000000142, 9.722557227176030992 ) ) ;
#112306=EDGE_CURVE ( 'NONE', #80065, #81768, #51100, .T. ) ;
#112307=ORIENTED_EDGE ( 'NONE', *, *, #34640, .F. ) ;
#112308=LINE ( 'NONE', #86970, #85800 ) ;
#112309=ORIENTED_EDGE ( 'NONE', *, *, #23839, .F. ) ;
#112310=LINE ( 'NONE', #56543, #137174 ) ;
#112311=EDGE_CURVE ( 'NONE', #35940, #26671, #60572, .T. ) ;
#112313=EDGE_LOOP ( 'NONE', ( #64830, #92810, #49677, #118818 ) ) ;
#112317=ORIENTED_EDGE ( 'NONE', *, *, #115448, .F. ) ;
#112318=ORIENTED_EDGE ( 'NONE', *, *, #81875, .F. ) ;
#112320=DIRECTION ( 'NONE',  ( 0.7071067811865486830, -0.7071067811865464625, -0.000000000000000000 ) ) ;
#112321=DIRECTION ( 'NONE',  ( -0.7071067811865487940, 0.7071067811865463515, -0.000000000000000000 ) ) ;
#112322=DIRECTION ( 'NONE',  ( -0.7071067811865486830, -0.7071067811865464625, -0.000000000000000000 ) ) ;
#112323=CARTESIAN_POINT ( 'NONE',  ( -18.18398860626898994, 28.73617430169800002, 5.000000000000000000 ) ) ;
#112324=ORIENTED_EDGE ( 'NONE', *, *, #114218, .T. ) ;
#112326=DIRECTION ( 'NONE',  ( -0.000000000000000000, -0.3543493200069152693, 0.9351131265310292928 ) ) ;
#112327=DIRECTION ( 'NONE',  ( 0.7071067811865487940, 0.7071067811865463515, 0.000000000000000000 ) ) ;
#112328=ORIENTED_EDGE ( 'NONE', *, *, #119971, .F. ) ;
#112330=FACE_OUTER_BOUND ( 'NONE', #9082, .T. ) ;
#112331=EDGE_LOOP ( 'NONE', ( #40722, #14781, #113876, #92852 ) ) ;
#112333=VERTEX_POINT ( 'NONE', #128646 ) ;
#112334=ORIENTED_EDGE ( 'NONE', *, *, #72882, .T. ) ;
#112335=ADVANCED_FACE ( 'NONE', ( #15551 ), #30029, .F. ) ;
#112336=DIRECTION ( 'NONE',  ( -0.000000000000000000, 0.000000000000000000, 1.000000000000000000 ) ) ;
#112337=FACE_OUTER_BOUND ( 'NONE', #89751, .T. ) ;
#112340=ORIENTED_EDGE ( 'NONE', *, *, #50119, .T. ) ;
#112342=CARTESIAN_POINT ( 'NONE',  ( 83.99451991528748351, 28.92564299267996830, 4.000000000000000000 ) ) ;
#112343=VECTOR ( 'NONE', #7123, 1000.000000000000000 ) ;
#112344=DIRECTION ( 'NONE',  ( 0.7071067811865486830, -0.7071067811865464625, -0.000000000000000000 ) ) ;
#112345=LINE ( 'NONE', #24606, #97016 ) ;
#112346=AXIS2_PLACEMENT_3D ( 'NONE', #94706, #15697, #28783 ) ;
#112347=CARTESIAN_POINT ( 'NONE',  ( 34.49999999999975842, 6.054329344830883031, 4.994342998332162331 ) ) ;
#112348=CARTESIAN_POINT ( 'NONE',  ( 34.42499999999998295, 0.000000000000000000, 4.500000000000000888 ) ) ;
#112349=CARTESIAN_POINT ( 'NONE',  ( 27.00548008471251293, 28.92564299267919381, 4.000000000000000000 ) ) ;
#112350=EDGE_CURVE ( 'NONE', #20421, #122494, #127950, .T. ) ;
#112351=CARTESIAN_POINT ( 'NONE',  ( 0.000000000000000000, 0.000000000000000000, 5.000000000000000000 ) ) ;
#112353=CARTESIAN_POINT ( 'NONE',  ( 48.29974487139158867, -27.71228299555239971, 4.000000000000000000 ) ) ;
#112354=CARTESIAN_POINT ( 'NONE',  ( -17.99999999999986855, -3.033600742197710254, 5.000000000000000000 ) ) ;
#112355=FACE_OUTER_BOUND ( 'NONE', #21383, .T. ) ;
#112356=EDGE_LOOP ( 'NONE', ( #118536, #43743, #140569, #37621 ) ) ;
#112357=ORIENTED_EDGE ( 'NONE', *, *, #17378, .F. ) ;
#112359=ORIENTED_EDGE ( 'NONE', *, *, #91541, .F. ) ;
#112360=VECTOR ( 'NONE', #54415, 1000.000000000000000 ) ;
#112361=ORIENTED_EDGE ( 'NONE', *, *, #101227, .F. ) ;
#112362=ADVANCED_FACE ( 'NONE', ( #93866 ), #48961, .T. ) ;
#112364=CARTESIAN_POINT ( 'NONE',  ( 4.499999999999968914, -9.462702396501006419, -9.474982329943523851 ) ) ;
#112365=DIRECTION ( 'NONE',  ( -0.7071067811865486830, -0.7071067811865464625, 0.000000000000000000 ) ) ;
#112366=DIRECTION ( 'NONE',  ( -0.000000000000000000, 0.000000000000000000, 1.000000000000000000 ) ) ;
#112367=ORIENTED_EDGE ( 'NONE', *, *, #117660, .T. ) ;
#112368=CARTESIAN_POINT ( 'NONE',  ( 17.99999999999987566, -21.03360074219752462, 5.000000000000000000 ) ) ;
#112370=DIRECTION ( 'NONE',  ( 0.000000000000000000, 1.000000000000000000, 0.000000000000000000 ) ) ;
#112371=DIRECTION ( 'NONE',  ( -8.817971600062199903E-18, 0.3543493200069153248, 0.9351131265310292928 ) ) ;
#112372=EDGE_CURVE ( 'NONE', #71967, #115239, #18414, .T. ) ;
#112373=ORIENTED_EDGE ( 'NONE', *, *, #37225, .F. ) ;
#112374=DIRECTION ( 'NONE',  ( 0.3543493200069162685, -0.000000000000000000, -0.9351131265310288487 ) ) ;
#112376=FACE_OUTER_BOUND ( 'NONE', #86168, .T. ) ;
#112378=CARTESIAN_POINT ( 'NONE',  ( 16.37176554955605567, -8.240707523384193323, 11.38925528200748971 ) ) ;
#112379=CARTESIAN_POINT ( 'NONE',  ( 15.71230993966017664, -21.73547319004781286, 4.999917730833664642 ) ) ;
#112380=CARTESIAN_POINT ( 'NONE',  ( 34.49999999999976552, -11.56887692260769640, 4.000000000000000000 ) ) ;
#112381=PLANE ( 'NONE',  #31352 ) ;
#112382=VECTOR ( 'NONE', #138405, 1000.000000000000227 ) ;
#112383=LINE ( 'NONE', #55879, #7515 ) ;
#112384=ORIENTED_EDGE ( 'NONE', *, *, #120122, .F. ) ;
#112385=ORIENTED_EDGE ( 'NONE', *, *, #18143, .F. ) ;
#112386=VECTOR ( 'NONE', #114838, 999.9999999999998863 ) ;
#112389=VECTOR ( 'NONE', #135603, 999.9999999999998863 ) ;
#112390=EDGE_CURVE ( 'NONE', #28496, #117668, #40929, .T. ) ;
#112391=CARTESIAN_POINT ( 'NONE',  ( -81.18398860626899705, 28.73617430169844056, 5.000000000000000000 ) ) ;
#112393=EDGE_CURVE ( 'NONE', #49213, #60654, #138096, .T. ) ;
#112394=FACE_OUTER_BOUND ( 'NONE', #133546, .T. ) ;
#112395=DIRECTION ( 'NONE',  ( -0.7071067811865486830, -0.7071067811865464625, -0.000000000000000000 ) ) ;
#112397=ORIENTED_EDGE ( 'NONE', *, *, #4882, .T. ) ;
#112398=ORIENTED_EDGE ( 'NONE', *, *, #84852, .F. ) ;
#112400=ADVANCED_FACE ( 'NONE', ( #132961 ), #53971, .F. ) ;
#112401=DIRECTION ( 'NONE',  ( 0.7071067811865487940, 0.7071067811865463515, -0.000000000000000000 ) ) ;
#112402=VERTEX_POINT ( 'NONE', #130081 ) ;
#112404=VERTEX_POINT ( 'NONE', #96687 ) ;
#112409=VERTEX_POINT ( 'NONE', #21314 ) ;
#112410=ORIENTED_EDGE ( 'NONE', *, *, #33764, .T. ) ;
#112411=EDGE_CURVE ( 'NONE', #128596, #88238, #22008, .T. ) ;
#112412=CARTESIAN_POINT ( 'NONE',  ( -26.28769006033953559, -21.73547319004780931, 4.999917730833664642 ) ) ;
#112416=ADVANCED_FACE ( 'NONE', ( #109742 ), #97418, .F. ) ;
#112417=EDGE_CURVE ( 'NONE', #13922, #45110, #19169, .T. ) ;
#112418=CARTESIAN_POINT ( 'NONE',  ( -5.816011393731002066, 28.73617430169783304, 5.000000000000000000 ) ) ;
#112420=LINE ( 'NONE', #14531, #19010 ) ;
#112422=FACE_OUTER_BOUND ( 'NONE', #16131, .T. ) ;
#112424=EDGE_CURVE ( 'NONE', #118741, #56485, #63427, .T. ) ;
#112425=DIRECTION ( 'NONE',  ( -0.7071067811865486830, -0.7071067811865464625, 0.000000000000000000 ) ) ;
#112426=FACE_BOUND ( 'NONE', #39568, .T. ) ;
#112427=EDGE_CURVE ( 'NONE', #110220, #117528, #66258, .T. ) ;
#112428=ORIENTED_EDGE ( 'NONE', *, *, #100954, .T. ) ;
#112429=DIRECTION ( 'NONE',  ( -0.7071067811865487940, 0.7071067811865463515, -0.000000000000000000 ) ) ;
#112430=DIRECTION ( 'NONE',  ( -0.000000000000000000, -0.3543493200069153803, -0.9351131265310292928 ) ) ;
#112431=CARTESIAN_POINT ( 'NONE',  ( -34.42500000000001137, -1.458600742197974087, 5.000000000000000000 ) ) ;
#112432=ADVANCED_FACE ( 'NONE', ( #52500 ), #9703, .F. ) ;
#112433=VERTEX_POINT ( 'NONE', #119182 ) ;
#112434=CARTESIAN_POINT ( 'NONE',  ( 57.18398860626899705, 28.73617430169827358, 5.000000000000000000 ) ) ;
#112435=ORIENTED_EDGE ( 'NONE', *, *, #39889, .T. ) ;
#112436=EDGE_LOOP ( 'NONE', ( #91452, #87080, #129756, #113134 ) ) ;
#112437=( BOUNDED_CURVE ( )  B_SPLINE_CURVE ( 3, ( #11568, #32659, #132713, #65302 ),
 .UNSPECIFIED., .F., .T. ) 
 B_SPLINE_CURVE_WITH_KNOTS ( ( 4, 4 ),
 ( 1.964434688349483871, 3.503810798801452187 ),
 .UNSPECIFIED. ) 
 CURVE ( )  GEOMETRIC_REPRESENTATION_ITEM ( )  RATIONAL_B_SPLINE_CURVE ( ( 1.000000000000000000, 0.8120851936182270636, 0.8120851936182270636, 1.000000000000000000 ) ) 
 REPRESENTATION_ITEM ( '' )  );
#112439=VECTOR ( 'NONE', #107724, 1000.000000000000000 ) ;
#112445=VECTOR ( 'NONE', #8395, 1000.000000000000227 ) ;
#112449=DIRECTION ( 'NONE',  ( 0.7071067811865487940, 0.7071067811865463515, -0.000000000000000000 ) ) ;
#112450=EDGE_CURVE ( 'NONE', #123033, #8173, #19868, .T. ) ;
#112451=DIRECTION ( 'NONE',  ( -0.6830127018922181881, 0.6830127018922202975, -0.2588190451025214056 ) ) ;
#112452=VECTOR ( 'NONE', #23725, 999.9999999999998863 ) ;
#112453=DIRECTION ( 'NONE',  ( -0.3543493200069162685, -0.000000000000000000, -0.9351131265310288487 ) ) ;
#112454=DIRECTION ( 'NONE',  ( -0.6830127018922181881, 0.6830127018922202975, -0.2588190451025214056 ) ) ;
#112455=ORIENTED_EDGE ( 'NONE', *, *, #43880, .F. ) ;
#112456=ORIENTED_EDGE ( 'NONE', *, *, #29548, .T. ) ;
#112457=EDGE_CURVE ( 'NONE', #121270, #115355, #130814, .T. ) ;
#112459=ORIENTED_EDGE ( 'NONE', *, *, #125688, .T. ) ;
#112460=CARTESIAN_POINT ( 'NONE',  ( -35.99451991528749772, 28.92564299267963079, 4.000000000000000000 ) ) ;
#112463=PLANE ( 'NONE',  #30526 ) ;
#112464=CARTESIAN_POINT ( 'NONE',  ( -4.499999999999968914, 11.52377502935402198, -1.522421517564075399 ) ) ;
#112465=ORIENTED_EDGE ( 'NONE', *, *, #89786, .T. ) ;
#112466=DIRECTION ( 'NONE',  ( -0.000000000000000000, 0.3543493200069152138, -0.9351131265310292928 ) ) ;
#112467=VECTOR ( 'NONE', #67855, 1000.000000000000000 ) ;
#112468=EDGE_CURVE ( 'NONE', #116410, #29922, #55383, .T. ) ;
#112472=VECTOR ( 'NONE', #128451, 1000.000000000000000 ) ;
#112473=PLANE ( 'NONE',  #69352 ) ;
#112474=ORIENTED_EDGE ( 'NONE', *, *, #134238, .T. ) ;
#112476=VECTOR ( 'NONE', #71130, 999.9999999999998863 ) ;
#112479=DIRECTION ( 'NONE',  ( 0.7071067811865486830, -0.7071067811865464625, -0.000000000000000000 ) ) ;
#112480=DIRECTION ( 'NONE',  ( 0.6830127018922180770, -0.6830127018922204085, -0.2588190451025213501 ) ) ;
#112481=ORIENTED_EDGE ( 'NONE', *, *, #3855, .F. ) ;
#112482=DIRECTION ( 'NONE',  ( -0.6830127018922181881, 0.6830127018922202975, -0.2588190451025214056 ) ) ;
#112483=ORIENTED_EDGE ( 'NONE', *, *, #122029, .T. ) ;
#112484=DIRECTION ( 'NONE',  ( 0.7071067811865487940, -0.7071067811865463515, 0.000000000000000000 ) ) ;
#112486=DIRECTION ( 'NONE',  ( 0.7071067811865487940, 0.7071067811865463515, 0.000000000000000000 ) ) ;
#112487=DIRECTION ( 'NONE',  ( -0.7071067811865487940, 0.7071067811865463515, -0.000000000000000000 ) ) ;
#112489=CARTESIAN_POINT ( 'NONE',  ( 15.01966765291686734, -22.22500000000000142, -13.92590160340912853 ) ) ;
#112490=FACE_OUTER_BOUND ( 'NONE', #75154, .T. ) ;
#112491=CARTESIAN_POINT ( 'NONE',  ( -3.489213562373097322, -27.52281430457057709, 5.000000000000000000 ) ) ;
#112493=CARTESIAN_POINT ( 'NONE',  ( 2.999999999999975131, 12.83542986846997458, -1.025386466790376927 ) ) ;
#112494=VERTEX_POINT ( 'NONE', #135108 ) ;
#112495=LINE ( 'NONE', #77040, #18291 ) ;
#112496=FACE_OUTER_BOUND ( 'NONE', #114557, .T. ) ;
#112497=ORIENTED_EDGE ( 'NONE', *, *, #102947, .T. ) ;
#112498=ORIENTED_EDGE ( 'NONE', *, *, #86418, .F. ) ;
#112499=DIRECTION ( 'NONE',  ( -1.000000000000000000, 0.000000000000000000, 0.000000000000000000 ) ) ;
#112500=LINE ( 'NONE', #57429, #71403 ) ;
#112501=EDGE_LOOP ( 'NONE', ( #137860, #122668, #78729, #47260 ) ) ;
#112502=PLANE ( 'NONE',  #87643 ) ;
#112503=PLANE ( 'NONE',  #120177 ) ;
#112504=DIRECTION ( 'NONE',  ( -0.7071067811865486830, 0.7071067811865464625, 0.000000000000000000 ) ) ;
#112506=DIRECTION ( 'NONE',  ( -0.7071067811865486830, 0.7071067811865464625, -0.000000000000000000 ) ) ;
#112507=EDGE_CURVE ( 'NONE', #58911, #46933, #36472, .T. ) ;
#112508=DIRECTION ( 'NONE',  ( 0.7071067811865486830, -0.7071067811865464625, -0.000000000000000000 ) ) ;
#112509=EDGE_CURVE ( 'NONE', #69167, #44746, #92254, .T. ) ;
#112510=CARTESIAN_POINT ( 'NONE',  ( -5.207106781186500832, -8.240707523384196875, 5.000000000000000000 ) ) ;
#112511=CARTESIAN_POINT ( 'NONE',  ( -1.499999999999994449, -14.70932175296477418, -11.46312253303836926 ) ) ;
#112512=LINE ( 'NONE', #125549, #131668 ) ;
#112513=LINE ( 'NONE', #68342, #7184 ) ;
#112515=EDGE_LOOP ( 'NONE', ( #78985, #27950, #28952, #19372 ) ) ;
#112517=CARTESIAN_POINT ( 'NONE',  ( 3.005480084712505828, 28.92564299267936079, 4.000000000000000000 ) ) ;
#112519=ORIENTED_EDGE ( 'NONE', *, *, #104905, .T. ) ;
#112520=ORIENTED_EDGE ( 'NONE', *, *, #98642, .T. ) ;
#112521=FACE_OUTER_BOUND ( 'NONE', #15245, .T. ) ;
#112522=CARTESIAN_POINT ( 'NONE',  ( -8.483345613589495571, 22.22500000000000142, 4.500000000000000888 ) ) ;
#112523=VERTEX_POINT ( 'NONE', #124191 ) ;
#112525=CARTESIAN_POINT ( 'NONE',  ( 0.000000000000000000, 0.000000000000000000, 5.000000000000000000 ) ) ;
#112526=EDGE_CURVE ( 'NONE', #124292, #67057, #22694, .T. ) ;
#112527=DIRECTION ( 'NONE',  ( -0.6830127018922181881, 0.6830127018922202975, -0.2588190451025214056 ) ) ;
#112528=LINE ( 'NONE', #101644, #88110 ) ;
#112530=EDGE_CURVE ( 'NONE', #75880, #105769, #123515, .T. ) ;
#112531=VERTEX_POINT ( 'NONE', #58992 ) ;
#112532=LINE ( 'NONE', #136415, #7075 ) ;
#112536=LINE ( 'NONE', #80641, #59097 ) ;
#112537=LINE ( 'NONE', #93652, #49205 ) ;
#112538=PLANE ( 'NONE',  #94418 ) ;
#112539=EDGE_CURVE ( 'NONE', #40982, #445, #80015, .T. ) ;
#112541=EDGE_CURVE ( 'NONE', #5483, #89397, #45243, .T. ) ;
#112542=VECTOR ( 'NONE', #92762, 1000.000000000000000 ) ;
#112544=CARTESIAN_POINT ( 'NONE',  ( -4.171830600776443632, -11.24070752338417556, 4.000000000000000000 ) ) ;
#112545=VERTEX_POINT ( 'NONE', #91568 ) ;
#112546=VERTEX_POINT ( 'NONE', #961 ) ;
#112548=ORIENTED_EDGE ( 'NONE', *, *, #135777, .T. ) ;
#112549=VECTOR ( 'NONE', #76033, 1000.000000000000227 ) ;
#112552=EDGE_LOOP ( 'NONE', ( #59660, #92648, #84965, #115067, #86787 ) ) ;
#112553=FACE_OUTER_BOUND ( 'NONE', #116477, .T. ) ;
#112554=CARTESIAN_POINT ( 'NONE',  ( -5.999999999999956479, -9.412538124160663600, 4.000000000000000000 ) ) ;
#112555=ADVANCED_FACE ( 'NONE', ( #133652 ), #33641, .F. ) ;
#112557=AXIS2_PLACEMENT_3D ( 'NONE', #38018, #138750, #82937 ) ;
#112558=ORIENTED_EDGE ( 'NONE', *, *, #66035, .T. ) ;
#112559=FACE_OUTER_BOUND ( 'NONE', #28850, .T. ) ;
#112560=VERTEX_POINT ( 'NONE', #102465 ) ;
#112561=CARTESIAN_POINT ( 'NONE',  ( 30.32816939922332367, 11.25929247661560773, 4.000000000000000000 ) ) ;
#112562=EDGE_CURVE ( 'NONE', #34094, #88720, #14717, .T. ) ;
#112564=CARTESIAN_POINT ( 'NONE',  ( -21.70710678118638626, -3.740707523384246613, 5.000000000000000000 ) ) ;
#112566=ORIENTED_EDGE ( 'NONE', *, *, #68214, .T. ) ;
#112567=VECTOR ( 'NONE', #67295, 1000.000000000000000 ) ;
#112568=CARTESIAN_POINT ( 'NONE',  ( 31.17183060077625711, 0.7592924766157104211, 4.000000000000000000 ) ) ;
#112569=ORIENTED_EDGE ( 'NONE', *, *, #89811, .T. ) ;
#112570=PLANE ( 'NONE',  #35478 ) ;
#112571=CARTESIAN_POINT ( 'NONE',  ( -34.92500000000001137, -9.415263340095652467, 16.98967855471612509 ) ) ;
#112572=CARTESIAN_POINT ( 'NONE',  ( 9.183988606268997046, 28.73617430169793607, 5.000000000000000000 ) ) ;
#112575=CARTESIAN_POINT ( 'NONE',  ( 24.48921356237309510, -27.52281430457072631, 5.000000000000000000 ) ) ;
#112576=EDGE_CURVE ( 'NONE', #43058, #54084, #122025, .T. ) ;
#112577=VECTOR ( 'NONE', #22664, 1000.000000000000000 ) ;
#112578=VECTOR ( 'NONE', #100804, 1000.000000000000000 ) ;
#112582=FACE_OUTER_BOUND ( 'NONE', #70233, .T. ) ;
#112583=EDGE_CURVE ( 'NONE', #60173, #102939, #1656, .T. ) ;
#112584=CARTESIAN_POINT ( 'NONE',  ( 39.48921356237310221, -27.52281430457082934, 5.000000000000000000 ) ) ;
#112585=PLANE ( 'NONE',  #68812 ) ;
#112586=ORIENTED_EDGE ( 'NONE', *, *, #44494, .F. ) ;
#112587=ORIENTED_EDGE ( 'NONE', *, *, #6273, .F. ) ;
#112588=VECTOR ( 'NONE', #142837, 1000.000000000000227 ) ;
#112589=LINE ( 'NONE', #80000, #77133 ) ;
#112590=ORIENTED_EDGE ( 'NONE', *, *, #140798, .F. ) ;
#112592=EDGE_CURVE ( 'NONE', #101850, #117764, #23442, .T. ) ;
#112593=CARTESIAN_POINT ( 'NONE',  ( 11.51078643762690490, -27.52281430457047406, 5.000000000000000000 ) ) ;
#112594=ADVANCED_FACE ( 'NONE', ( #45941 ), #69854, .T. ) ;
#112595=ORIENTED_EDGE ( 'NONE', *, *, #106155, .F. ) ;
#112596=PLANE ( 'NONE',  #12132 ) ;
#112597=CARTESIAN_POINT ( 'NONE',  ( -34.92500000000001137, -2.143876922607542035, 4.000000000000000000 ) ) ;
#112598=EDGE_CURVE ( 'NONE', #103813, #114933, #111900, .T. ) ;
#112599=DIRECTION ( 'NONE',  ( -0.000000000000000000, 0.3543493200069153248, 0.9351131265310292928 ) ) ;
#112600=FACE_BOUND ( 'NONE', #141335, .T. ) ;
#112601=EDGE_CURVE ( 'NONE', #40143, #133528, #38616, .T. ) ;
#112602=PLANE ( 'NONE',  #96559 ) ;
#112603=PLANE ( 'NONE',  #97730 ) ;
#112604=DIRECTION ( 'NONE',  ( -0.000000000000000000, 0.000000000000000000, 1.000000000000000000 ) ) ;
#112605=CARTESIAN_POINT ( 'NONE',  ( 2.999999999999981792, 10.21212019023809781, -2.019456568337804292 ) ) ;
#112606=ORIENTED_EDGE ( 'NONE', *, *, #92850, .F. ) ;
#112607=CARTESIAN_POINT ( 'NONE',  ( -39.48921356237310221, -27.52281430457082934, 5.000000000000000000 ) ) ;
#112608=ORIENTED_EDGE ( 'NONE', *, *, #24534, .F. ) ;
#112609=ORIENTED_EDGE ( 'NONE', *, *, #21616, .T. ) ;
#112611=ORIENTED_EDGE ( 'NONE', *, *, #99707, .T. ) ;
#112612=EDGE_CURVE ( 'NONE', #49875, #100624, #61815, .T. ) ;
#112613=CARTESIAN_POINT ( 'NONE',  ( 17.67183060077634593, 20.25929247661551003, 4.000000000000000000 ) ) ;
#112614=ORIENTED_EDGE ( 'NONE', *, *, #82602, .F. ) ;
#112615=CARTESIAN_POINT ( 'NONE',  ( -21.48921356237309155, -27.52281430457070499, 5.000000000000000000 ) ) ;
#112616=AXIS2_PLACEMENT_3D ( 'NONE', #54965, #133938, #122315 ) ;
#112617=EDGE_CURVE ( 'NONE', #41413, #99874, #59673, .T. ) ;
#112618=LINE ( 'NONE', #88748, #44955 ) ;
#112619=DIRECTION ( 'NONE',  ( -0.6830127018922181881, 0.6830127018922202975, -0.2588190451025214056 ) ) ;
#112620=CARTESIAN_POINT ( 'NONE',  ( -34.47516574401891631, 10.49051761211550726, 4.998110765256836174 ) ) ;
#112621=DIRECTION ( 'NONE',  ( -0.000000000000000000, 0.000000000000000000, 1.000000000000000000 ) ) ;
#112623=CARTESIAN_POINT ( 'NONE',  ( -8.999999999999934275, 4.931123077392131293, 4.000000000000000000 ) ) ;
#112624=FACE_OUTER_BOUND ( 'NONE', #77446, .T. ) ;
#112626=VECTOR ( 'NONE', #84379, 1000.000000000000000 ) ;
#112627=ORIENTED_EDGE ( 'NONE', *, *, #37606, .T. ) ;
#112628=CARTESIAN_POINT ( 'NONE',  ( -13.49999999999990230, 18.05218569542898521, 5.000000000000000000 ) ) ;
#112630=ORIENTED_EDGE ( 'NONE', *, *, #18424, .T. ) ;
#112631=ORIENTED_EDGE ( 'NONE', *, *, #115942, .F. ) ;
#112632=VERTEX_POINT ( 'NONE', #49525 ) ;
#112635=CARTESIAN_POINT ( 'NONE',  ( 0.000000000000000000, 0.000000000000000000, 5.000000000000000000 ) ) ;
#112636=VECTOR ( 'NONE', #27918, 1000.000000000000000 ) ;
#112637=EDGE_CURVE ( 'NONE', #19510, #103200, #95116, .T. ) ;
#112638=LINE ( 'NONE', #25616, #67540 ) ;
#112640=DIRECTION ( 'NONE',  ( -0.7071067811865486830, 0.7071067811865464625, 0.000000000000000000 ) ) ;
#112641=VERTEX_POINT ( 'NONE', #81436 ) ;
#112642=VECTOR ( 'NONE', #54311, 1000.000000000000000 ) ;
#112643=DIRECTION ( 'NONE',  ( 1.000000000000000000, 0.000000000000000000, 0.000000000000000000 ) ) ;
#112644=CARTESIAN_POINT ( 'NONE',  ( -12.48921356237309155, -27.52281430457064104, 5.000000000000000000 ) ) ;
#112645=LINE ( 'NONE', #2423, #10416 ) ;
#112646=DIRECTION ( 'NONE',  ( 0.7071067811865487940, 0.7071067811865463515, 0.000000000000000000 ) ) ;
#112647=ORIENTED_EDGE ( 'NONE', *, *, #79086, .F. ) ;
#112648=ORIENTED_EDGE ( 'NONE', *, *, #65616, .T. ) ;
#112650=DIRECTION ( 'NONE',  ( 0.3543493200069162685, -0.000000000000000000, -0.9351131265310288487 ) ) ;
#112651=LINE ( 'NONE', #25630, #77207 ) ;
#112652=ORIENTED_EDGE ( 'NONE', *, *, #54945, .F. ) ;
#112653=FACE_OUTER_BOUND ( 'NONE', #54799, .T. ) ;
#112654=CARTESIAN_POINT ( 'NONE',  ( -0.7061230773919507930, 22.22500000000000142, 4.000000000000000000 ) ) ;
#112658=CARTESIAN_POINT ( 'NONE',  ( 54.48921356237310221, -27.52281430457093236, 5.000000000000000000 ) ) ;
#112659=CARTESIAN_POINT ( 'NONE',  ( 8.999999999999934275, 10.21212019023809425, -2.019456568337821611 ) ) ;
#112660=FACE_OUTER_BOUND ( 'NONE', #85968, .T. ) ;
#112661=DIRECTION ( 'NONE',  ( -0.000000000000000000, -0.3543493200069152693, 0.9351131265310292928 ) ) ;
#112662=LINE ( 'NONE', #124253, #42444 ) ;
#112664=CARTESIAN_POINT ( 'NONE',  ( 71.99451991528749772, 28.92564299267988304, 4.000000000000000000 ) ) ;
#112665=ORIENTED_EDGE ( 'NONE', *, *, #106503, .T. ) ;
#112666=ORIENTED_EDGE ( 'NONE', *, *, #10555, .T. ) ;
#112668=CARTESIAN_POINT ( 'NONE',  ( 21.79333936457832266, 21.75929247661549226, 4.998822639870715179 ) ) ;
#112669=VECTOR ( 'NONE', #86012, 1000.000000000000000 ) ;
#112670=DIRECTION ( 'NONE',  ( -0.3543493200069163240, 4.681814790819596721E-17, -0.9351131265310288487 ) ) ;
#112672=VECTOR ( 'NONE', #68702, 1000.000000000000000 ) ;
#112673=ORIENTED_EDGE ( 'NONE', *, *, #25788, .T. ) ;
#112674=CARTESIAN_POINT ( 'NONE',  ( -25.49999999999981881, -8.947814304570739452, 5.000000000000000000 ) ) ;
#112675=DIRECTION ( 'NONE',  ( 0.7071067811865486830, -0.7071067811865464625, -0.000000000000000000 ) ) ;
#112678=CARTESIAN_POINT ( 'NONE',  ( -8.999999999999932498, 1.761378380278673994, -6.096875308897274692 ) ) ;
#112679=VECTOR ( 'NONE', #129629, 1000.000000000000000 ) ;
#112681=CARTESIAN_POINT ( 'NONE',  ( -63.29974487139158867, -27.71228299555250274, 4.000000000000000000 ) ) ;
#112682=EDGE_CURVE ( 'NONE', #72848, #62221, #125637, .T. ) ;
#112683=CARTESIAN_POINT ( 'NONE',  ( 34.60428828362104525, 22.19175015946030172, 4.000000000000000000 ) ) ;
#112684=LINE ( 'NONE', #13352, #51081 ) ;
#112685=VERTEX_POINT ( 'NONE', #93710 ) ;
#112687=EDGE_CURVE ( 'NONE', #88279, #95024, #26315, .T. ) ;
#112688=EDGE_CURVE ( 'NONE', #116339, #103979, #138651, .T. ) ;
#112689=ORIENTED_EDGE ( 'NONE', *, *, #136762, .F. ) ;
#112690=CARTESIAN_POINT ( 'NONE',  ( 34.49999999999976552, 0.4311230773921780335, 4.000000000000000000 ) ) ;
#112693=EDGE_CURVE ( 'NONE', #62248, #78479, #70572, .T. ) ;
#112696=CARTESIAN_POINT ( 'NONE',  ( -7.499999999999940492, -11.94781430457070925, 5.000000000000000000 ) ) ;
#112698=EDGE_CURVE ( 'NONE', #110453, #76657, #15390, .T. ) ;
#112699=EDGE_LOOP ( 'NONE', ( #37462, #96463, #17072, #91770 ) ) ;
#112700=EDGE_LOOP ( 'NONE', ( #98213, #90353, #109701, #102623 ) ) ;
#112701=DIRECTION ( 'NONE',  ( 0.7071067811865487940, -0.7071067811865463515, 0.000000000000000000 ) ) ;
#112702=CARTESIAN_POINT ( 'NONE',  ( -24.18398860626899705, 28.73617430169804265, 5.000000000000000000 ) ) ;
#112704=CARTESIAN_POINT ( 'NONE',  ( 8.207106781186487510, -8.240707523384203981, 5.000000000000000000 ) ) ;
#112706=EDGE_CURVE ( 'NONE', #77481, #86073, #6641, .T. ) ;
#112708=EDGE_CURVE ( 'NONE', #26671, #16046, #37921, .T. ) ;
#112709=CARTESIAN_POINT ( 'NONE',  ( -36.48921356237310221, -27.52281430457080802, 5.000000000000000000 ) ) ;
#112712=ORIENTED_EDGE ( 'NONE', *, *, #10098, .T. ) ;
#112714=DIRECTION ( 'NONE',  ( -0.7071067811865486830, -0.7071067811865464625, -0.000000000000000000 ) ) ;
#112715=EDGE_CURVE ( 'NONE', #63684, #7759, #16102, .T. ) ;
#112716=CARTESIAN_POINT ( 'NONE',  ( 78.48921356237309510, -27.52281430457109934, 5.000000000000000000 ) ) ;
#112717=DIRECTION ( 'NONE',  ( -0.7071067811865486830, -0.7071067811865464625, 0.000000000000000000 ) ) ;
#112718=VECTOR ( 'NONE', #17340, 1000.000000000000227 ) ;
#112720=ORIENTED_EDGE ( 'NONE', *, *, #96171, .F. ) ;
#112722=DIRECTION ( 'NONE',  ( -0.000000000000000000, -0.000000000000000000, 1.000000000000000000 ) ) ;
#112724=AXIS2_PLACEMENT_3D ( 'NONE', #14641, #62446, #39997 ) ;
#112725=EDGE_LOOP ( 'NONE', ( #33342, #124242, #142811, #3524 ) ) ;
#112726=ORIENTED_EDGE ( 'NONE', *, *, #1238, .F. ) ;
#112727=DIRECTION ( 'NONE',  ( -0.7071067811865486830, -0.7071067811865464625, 0.000000000000000000 ) ) ;
#112728=ADVANCED_FACE ( 'NONE', ( #5239 ), #27728, .T. ) ;
#112729=CARTESIAN_POINT ( 'NONE',  ( 57.18398860626899705, 28.73617430169827358, 5.000000000000000000 ) ) ;
#112730=FACE_OUTER_BOUND ( 'NONE', #111748, .T. ) ;
#112731=DIRECTION ( 'NONE',  ( 1.000000000000000000, -0.000000000000000000, -0.000000000000000000 ) ) ;
#112732=CARTESIAN_POINT ( 'NONE',  ( -69.29974487139159578, -27.71228299555254537, 4.000000000000000000 ) ) ;
#112733=ORIENTED_EDGE ( 'NONE', *, *, #63152, .T. ) ;
#112734=DIRECTION ( 'NONE',  ( 0.7071067811865487940, 0.7071067811865463515, 0.000000000000000000 ) ) ;
#112735=DIRECTION ( 'NONE',  ( 0.7071067811865487940, 0.7071067811865463515, 0.000000000000000000 ) ) ;
#112736=PLANE ( 'NONE',  #93365 ) ;
#112737=EDGE_CURVE ( 'NONE', #4524, #96941, #65748, .T. ) ;
#112738=LINE ( 'NONE', #57680, #71582 ) ;
#112739=ORIENTED_EDGE ( 'NONE', *, *, #78765, .F. ) ;
#112740=AXIS2_PLACEMENT_3D ( 'NONE', #5957, #115425, #27027 ) ;
#112741=ORIENTED_EDGE ( 'NONE', *, *, #129727, .T. ) ;
#112743=ORIENTED_EDGE ( 'NONE', *, *, #39238, .F. ) ;
#112744=VECTOR ( 'NONE', #122022, 1000.000000000000000 ) ;
#112745=LINE ( 'NONE', #143236, #135535 ) ;
#112746=CARTESIAN_POINT ( 'NONE',  ( 27.75860074219777118, 21.72500000000000142, 5.000000000000000000 ) ) ;
#112748=EDGE_CURVE ( 'NONE', #21912, #85379, #86024, .T. ) ;
#112749=LINE ( 'NONE', #101869, #55055 ) ;
#112750=LINE ( 'NONE', #114172, #29343 ) ;
#112751=ORIENTED_EDGE ( 'NONE', *, *, #88550, .T. ) ;
#112752=ORIENTED_EDGE ( 'NONE', *, *, #31053, .T. ) ;
#112755=ADVANCED_FACE ( 'NONE', ( #64274 ), #141856, .T. ) ;
#112756=ORIENTED_EDGE ( 'NONE', *, *, #77391, .F. ) ;
#112757=ADVANCED_FACE ( 'NONE', ( #53391 ), #97595, .F. ) ;
#112758=DIRECTION ( 'NONE',  ( -0.7071067811865487940, 0.7071067811865463515, -0.000000000000000000 ) ) ;
#112759=CARTESIAN_POINT ( 'NONE',  ( 14.56453960929607305, -0.7633378608190133363, 4.223415947001568860 ) ) ;
#112760=VERTEX_POINT ( 'NONE', #43250 ) ;
#112761=EDGE_CURVE ( 'NONE', #104374, #27773, #75181, .T. ) ;
#112762=FACE_BOUND ( 'NONE', #89912, .T. ) ;
#112764=CARTESIAN_POINT ( 'NONE',  ( -16.49999999999988276, -17.56887692260763956, 4.000000000000000000 ) ) ;
#112766=EDGE_CURVE ( 'NONE', #47526, #83800, #109911, .T. ) ;
#112767=AXIS2_PLACEMENT_3D ( 'NONE', #133642, #99549, #65299 ) ;
#112768=DIRECTION ( 'NONE',  ( 0.7071067811865487940, -0.7071067811865463515, 0.000000000000000000 ) ) ;
#112770=ORIENTED_EDGE ( 'NONE', *, *, #131111, .T. ) ;
#112771=VECTOR ( 'NONE', #71215, 1000.000000000000000 ) ;
#112774=ORIENTED_EDGE ( 'NONE', *, *, #9108, .T. ) ;
#112776=PLANE ( 'NONE',  #116061 ) ;
#112778=VECTOR ( 'NONE', #17330, 1000.000000000000000 ) ;
#112779=CARTESIAN_POINT ( 'NONE',  ( -30.48921356237309510, -27.52281430457076894, 5.000000000000000000 ) ) ;
#112780=CARTESIAN_POINT ( 'NONE',  ( -34.17183060077622514, -11.24070752338416135, 4.000000000000000000 ) ) ;
#112782=ORIENTED_EDGE ( 'NONE', *, *, #108251, .F. ) ;
#112783=PLANE ( 'NONE',  #13479 ) ;
#112784=CARTESIAN_POINT ( 'NONE',  ( -83.99451991528748351, 28.92564299267996830, 4.000000000000000000 ) ) ;
#112785=DIRECTION ( 'NONE',  ( 0.6830127018922180770, -0.6830127018922204085, -0.2588190451025213501 ) ) ;
#112787=LINE ( 'NONE', #100506, #2752 ) ;
#112789=CARTESIAN_POINT ( 'NONE',  ( -39.48921356237310221, -27.52281430457082934, 5.000000000000000000 ) ) ;
#112790=DIRECTION ( 'NONE',  ( -0.000000000000000000, 0.3543493200069153248, 0.9351131265310292928 ) ) ;
#112791=ORIENTED_EDGE ( 'NONE', *, *, #107533, .T. ) ;
#112792=EDGE_CURVE ( 'NONE', #32826, #85320, #42550, .T. ) ;
#112793=VERTEX_POINT ( 'NONE', #111327 ) ;
#112794=VERTEX_POINT ( 'NONE', #33118 ) ;
#112796=VECTOR ( 'NONE', #115618, 1000.000000000000227 ) ;
#112797=VERTEX_POINT ( 'NONE', #20752 ) ;
#112799=VECTOR ( 'NONE', #116875, 1000.000000000000000 ) ;
#112802=( BOUNDED_CURVE ( )  B_SPLINE_CURVE ( 3, ( #74582, #118770, #83309, #40523 ),
 .UNSPECIFIED., .F., .T. ) 
 B_SPLINE_CURVE_WITH_KNOTS ( ( 4, 4 ),
 ( 4.350170835173023498, 4.500739107949211615 ),
 .UNSPECIFIED. ) 
 CURVE ( )  GEOMETRIC_REPRESENTATION_ITEM ( )  RATIONAL_B_SPLINE_CURVE ( ( 1.000000000000000000, 0.9981116584018956406, 0.9981116584018956406, 1.000000000000000000 ) ) 
 REPRESENTATION_ITEM ( '' )  );
#112803=CARTESIAN_POINT ( 'NONE',  ( -34.42500000000001137, 19.54139925780181386, 5.000000000000000000 ) ) ;
#112804=ORIENTED_EDGE ( 'NONE', *, *, #28961, .F. ) ;
#112805=LINE ( 'NONE', #91087, #43282 ) ;
#112806=ORIENTED_EDGE ( 'NONE', *, *, #70204, .F. ) ;
#112807=LINE ( 'NONE', #59871, #102102 ) ;
#112808=VECTOR ( 'NONE', #47712, 1000.000000000000000 ) ;
#112809=CARTESIAN_POINT ( 'NONE',  ( 12.70701326429294831, -21.74070752338406365, 4.999753212805217117 ) ) ;
#112810=EDGE_LOOP ( 'NONE', ( #71844, #76226, #130236, #91888 ) ) ;
#112811=ADVANCED_FACE ( 'NONE', ( #120778 ), #77328, .F. ) ;
#112812=DIRECTION ( 'NONE',  ( -0.7071067811865487940, 0.7071067811865463515, -0.000000000000000000 ) ) ;
#112813=CARTESIAN_POINT ( 'NONE',  ( -24.99033360189226372, 3.759292476615678336, 4.478963035907990609 ) ) ;
#112815=ORIENTED_EDGE ( 'NONE', *, *, #142292, .T. ) ;
#112816=EDGE_CURVE ( 'NONE', #76633, #105676, #78017, .T. ) ;
#112817=LINE ( 'NONE', #12068, #99066 ) ;
#112818=ORIENTED_EDGE ( 'NONE', *, *, #1235, .T. ) ;
#112820=ORIENTED_EDGE ( 'NONE', *, *, #140363, .T. ) ;
#112821=CARTESIAN_POINT ( 'NONE',  ( 19.17183060077633883, 9.759292476615629042, 4.000000000000000000 ) ) ;
#112822=LINE ( 'NONE', #15607, #65409 ) ;
#112823=VECTOR ( 'NONE', #117914, 1000.000000000000000 ) ;
#112824=DIRECTION ( 'NONE',  ( -0.3543493200069162685, -0.000000000000000000, -0.9351131265310288487 ) ) ;
#112825=DIRECTION ( 'NONE',  ( -0.7071067811865487940, 0.7071067811865463515, -0.000000000000000000 ) ) ;
#112826=ADVANCED_FACE ( 'NONE', ( #65010 ), #31650, .T. ) ;
#112827=DIRECTION ( 'NONE',  ( 0.7071067811865487940, 0.7071067811865463515, 0.000000000000000000 ) ) ;
#112828=ORIENTED_EDGE ( 'NONE', *, *, #14611, .F. ) ;
#112831=DIRECTION ( 'NONE',  ( 0.3543493200069162685, -0.000000000000000000, -0.9351131265310288487 ) ) ;
#112832=CARTESIAN_POINT ( 'NONE',  ( 23.86500426248363027, 3.759292476615681888, 15.36553568819720716 ) ) ;
#112833=VECTOR ( 'NONE', #70568, 999.9999999999998863 ) ;
#112834=CARTESIAN_POINT ( 'NONE',  ( -2.999999999999975131, -22.06887692260758271, 4.000000000000000000 ) ) ;
#112835=ORIENTED_EDGE ( 'NONE', *, *, #59892, .T. ) ;
#112836=ORIENTED_EDGE ( 'NONE', *, *, #120519, .T. ) ;
#112839=FACE_OUTER_BOUND ( 'NONE', #34805, .T. ) ;
#112841=DIRECTION ( 'NONE',  ( -0.000000000000000000, -0.3543493200069152693, 0.9351131265310292928 ) ) ;
#112842=DIRECTION ( 'NONE',  ( 1.000000000000000000, 0.000000000000000000, 0.000000000000000000 ) ) ;
#112845=CARTESIAN_POINT ( 'NONE',  ( 12.77004279457784186, 21.73644205237998150, 5.000000000000000888 ) ) ;
#112847=DIRECTION ( 'NONE',  ( 0.7071067811865487940, 0.7071067811865463515, 0.000000000000000000 ) ) ;
#112849=ORIENTED_EDGE ( 'NONE', *, *, #69750, .T. ) ;
#112851=ORIENTED_EDGE ( 'NONE', *, *, #83584, .F. ) ;
#112852=VECTOR ( 'NONE', #83970, 1000.000000000000000 ) ;
#112853=PLANE ( 'NONE',  #66857 ) ;
#112854=CARTESIAN_POINT ( 'NONE',  ( -23.20710678118637915, -5.240707523384227073, 5.000000000000000000 ) ) ;
#112855=EDGE_LOOP ( 'NONE', ( #92835, #129566, #118454, #59503 ) ) ;
#112857=DIRECTION ( 'NONE',  ( 0.6830127018922180770, -0.6830127018922204085, -0.2588190451025213501 ) ) ;
#112858=EDGE_CURVE ( 'NONE', #18692, #81729, #133125, .T. ) ;
#112859=VERTEX_POINT ( 'NONE', #79486 ) ;
#112860=FACE_OUTER_BOUND ( 'NONE', #17389, .T. ) ;
#112861=ORIENTED_EDGE ( 'NONE', *, *, #76020, .T. ) ;
#112862=LINE ( 'NONE', #12825, #76873 ) ;
#112864=EDGE_LOOP ( 'NONE', ( #100061, #130033, #42935, #32244 ) ) ;
#112865=CIRCLE ( 'NONE', #55043, 0.5000000000000000000 ) ;
#112866=AXIS2_PLACEMENT_3D ( 'NONE', #94403, #26314, #82148 ) ;
#112867=DIRECTION ( 'NONE',  ( -0.7071067811865486830, -0.7071067811865464625, 0.000000000000000000 ) ) ;
#112869=EDGE_CURVE ( 'NONE', #49544, #47125, #1811, .T. ) ;
#112870=VECTOR ( 'NONE', #94009, 1000.000000000000000 ) ;
#112872=ADVANCED_FACE ( 'NONE', ( #101890 ), #12011, .F. ) ;
#112874=CARTESIAN_POINT ( 'NONE',  ( 20.20710678118641113, -11.24070752338416845, 5.000000000000000000 ) ) ;
#112875=EDGE_LOOP ( 'NONE', ( #60989, #24461, #23809, #78386 ) ) ;
#112876=ADVANCED_FACE ( 'NONE', ( #3275 ), #48225, .T. ) ;
#112877=CARTESIAN_POINT ( 'NONE',  ( -7.396568071053523319, -14.24070752338414358, 19.24067776001724539 ) ) ;
#112878=EDGE_CURVE ( 'NONE', #20530, #97534, #122939, .T. ) ;
#112881=CARTESIAN_POINT ( 'NONE',  ( 27.48921356237309155, -27.52281430457074762, 5.000000000000000000 ) ) ;
#112883=DIRECTION ( 'NONE',  ( -0.7071067811865486830, -0.7071067811865464625, 0.000000000000000000 ) ) ;
#112884=CARTESIAN_POINT ( 'NONE',  ( 31.56687199751238992, -21.74070752338405654, 6.915939825044000955 ) ) ;
#112885=EDGE_CURVE ( 'NONE', #50863, #62405, #56299, .T. ) ;
#112886=EDGE_LOOP ( 'NONE', ( #38275, #80402, #132059, #140980 ) ) ;
#112887=LINE ( 'NONE', #69404, #25813 ) ;
#112889=EDGE_LOOP ( 'NONE', ( #3291, #75229, #2636, #127925 ) ) ;
#112891=CARTESIAN_POINT ( 'NONE',  ( -63.48921356237309510, -27.52281430457099631, 5.000000000000000000 ) ) ;
#112892=DIRECTION ( 'NONE',  ( 0.3543493200069162685, -0.000000000000000000, -0.9351131265310288487 ) ) ;
#112893=DIRECTION ( 'NONE',  ( -0.7071067811865487940, 0.7071067811865463515, 0.000000000000000000 ) ) ;
#112894=ORIENTED_EDGE ( 'NONE', *, *, #53319, .F. ) ;
#112896=LINE ( 'NONE', #1257, #37269 ) ;
#112898=DIRECTION ( 'NONE',  ( -0.7071067811865486830, 0.7071067811865464625, 0.000000000000000000 ) ) ;
#112899=ORIENTED_EDGE ( 'NONE', *, *, #113230, .F. ) ;
#112900=EDGE_CURVE ( 'NONE', #69033, #135404, #135945, .T. ) ;
#112901=DIRECTION ( 'NONE',  ( -0.000000000000000000, -0.3543493200069152693, 0.9351131265310292928 ) ) ;
#112902=DIRECTION ( 'NONE',  ( -0.7071067811865487940, 0.7071067811865463515, 0.000000000000000000 ) ) ;
#112903=CARTESIAN_POINT ( 'NONE',  ( 18.29974487139159223, -27.71228299555219010, 4.000000000000000000 ) ) ;
#112904=VERTEX_POINT ( 'NONE', #70024 ) ;
#112905=DIRECTION ( 'NONE',  ( 0.7071067811865487940, 0.7071067811865463515, 0.000000000000000000 ) ) ;
#112906=AXIS2_PLACEMENT_3D ( 'NONE', #107633, #127997, #6858 ) ;
#112907=LINE ( 'NONE', #33939, #40768 ) ;
#112908=FACE_OUTER_BOUND ( 'NONE', #41867, .T. ) ;
#112909=LINE ( 'NONE', #55697, #40968 ) ;
#112910=EDGE_CURVE ( 'NONE', #65084, #57387, #35242, .T. ) ;
#112911=CARTESIAN_POINT ( 'NONE',  ( -16.49999999999988276, 10.94296225409025247, -9.576120664313295450 ) ) ;
#112912=ORIENTED_EDGE ( 'NONE', *, *, #141831, .T. ) ;
#112913=ORIENTED_EDGE ( 'NONE', *, *, #66274, .T. ) ;
#112914=ORIENTED_EDGE ( 'NONE', *, *, #87439, .F. ) ;
#112916=VECTOR ( 'NONE', #111603, 1000.000000000000000 ) ;
#112917=ORIENTED_EDGE ( 'NONE', *, *, #126790, .T. ) ;
#112918=CARTESIAN_POINT ( 'NONE',  ( -60.18398860626900415, 28.73617430169829490, 5.000000000000000000 ) ) ;
#112919=LINE ( 'NONE', #80325, #98839 ) ;
#112920=FACE_OUTER_BOUND ( 'NONE', #119293, .T. ) ;
#112921=CARTESIAN_POINT ( 'NONE',  ( 8.999999999999932498, -0.4125381241607412042, 4.000000000000000000 ) ) ;
#112922=ORIENTED_EDGE ( 'NONE', *, *, #79951, .F. ) ;
#112923=CARTESIAN_POINT ( 'NONE',  ( -53.99451991528749062, 28.92564299267975869, 4.000000000000000000 ) ) ;
#112924=DIRECTION ( 'NONE',  ( 0.7071067811865487940, 0.7071067811865463515, 0.000000000000000000 ) ) ;
#112926=ORIENTED_EDGE ( 'NONE', *, *, #66917, .T. ) ;
#112927=CARTESIAN_POINT ( 'NONE',  ( 36.48921356237310221, -27.52281430457080802, 5.000000000000000000 ) ) ;
#112928=EDGE_CURVE ( 'NONE', #77145, #31809, #133813, .T. ) ;
#112929=CARTESIAN_POINT ( 'NONE',  ( -13.49999999999990763, 10.94296225409025247, -9.576120664313284792 ) ) ;
#112930=ORIENTED_EDGE ( 'NONE', *, *, #39678, .T. ) ;
#112931=ORIENTED_EDGE ( 'NONE', *, *, #6004, .F. ) ;
#112932=DIRECTION ( 'NONE',  ( 0.000000000000000000, 0.000000000000000000, -1.000000000000000000 ) ) ;
#112935=DIRECTION ( 'NONE',  ( -0.6830127018922180770, -0.6830127018922204085, -0.2588190451025213501 ) ) ;
#112937=ADVANCED_FACE ( 'NONE', ( #57705 ), #59149, .F. ) ;
#112938=DIRECTION ( 'NONE',  ( 0.3543493200069163240, -0.000000000000000000, 0.9351131265310288487 ) ) ;
#112939=DIRECTION ( 'NONE',  ( -0.6830127018922181881, 0.6830127018922202975, -0.2588190451025214056 ) ) ;
#112940=ORIENTED_EDGE ( 'NONE', *, *, #127423, .T. ) ;
#112941=AXIS2_PLACEMENT_3D ( 'NONE', #49706, #93179, #117747 ) ;
#112942=ORIENTED_EDGE ( 'NONE', *, *, #83966, .T. ) ;
#112943=DIRECTION ( 'NONE',  ( -0.6830127018922180770, -0.6830127018922204085, -0.2588190451025213501 ) ) ;
#112944=ADVANCED_FACE ( 'NONE', ( #135269 ), #35955, .T. ) ;
#112945=ORIENTED_EDGE ( 'NONE', *, *, #46492, .T. ) ;
#112946=ORIENTED_EDGE ( 'NONE', *, *, #83510, .T. ) ;
#112947=VECTOR ( 'NONE', #48023, 1000.000000000000000 ) ;
#112949=ORIENTED_EDGE ( 'NONE', *, *, #34574, .T. ) ;
#112950=CARTESIAN_POINT ( 'NONE',  ( 4.499999999999971578, 22.01701374228155927, 2.453858888625620516 ) ) ;
#112951=DIRECTION ( 'NONE',  ( -0.7071067811865487940, 0.7071067811865463515, -0.000000000000000000 ) ) ;
#112953=PLANE ( 'NONE',  #138747 ) ;
#112954=AXIS2_PLACEMENT_3D ( 'NONE', #18468, #62747, #106931 ) ;
#112956=ORIENTED_EDGE ( 'NONE', *, *, #52070, .F. ) ;
#112958=VECTOR ( 'NONE', #82149, 1000.000000000000000 ) ;
#112959=ORIENTED_EDGE ( 'NONE', *, *, #46848, .T. ) ;
#112960=CARTESIAN_POINT ( 'NONE',  ( 34.42499999999998295, -21.72500000000000142, 0.4999999999999995559 ) ) ;
#112961=EDGE_CURVE ( 'NONE', #81784, #109346, #136652, .T. ) ;
#112962=ORIENTED_EDGE ( 'NONE', *, *, #115262, .T. ) ;
#112963=CARTESIAN_POINT ( 'NONE',  ( 34.42499999999998295, 22.22500000000000142, 5.000000000000000000 ) ) ;
#112964=VERTEX_POINT ( 'NONE', #86405 ) ;
#112965=DIRECTION ( 'NONE',  ( -0.000000000000000000, 0.000000000000000000, 1.000000000000000000 ) ) ;
#112967=ORIENTED_EDGE ( 'NONE', *, *, #75289, .T. ) ;
#112969=ORIENTED_EDGE ( 'NONE', *, *, #97898, .F. ) ;
#112971=CARTESIAN_POINT ( 'NONE',  ( -24.18398860626899705, 28.73617430169804265, 5.000000000000000000 ) ) ;
#112972=ADVANCED_FACE ( 'NONE', ( #108816 ), #131318, .T. ) ;
#112973=DIRECTION ( 'NONE',  ( -0.7071067811865487940, 0.7071067811865463515, -0.000000000000000000 ) ) ;
#112974=DIRECTION ( 'NONE',  ( -0.000000000000000000, 0.3543493200069153248, 0.9351131265310292928 ) ) ;
#112976=DIRECTION ( 'NONE',  ( -0.7071067811865486830, 0.7071067811865464625, 0.000000000000000000 ) ) ;
#112977=CARTESIAN_POINT ( 'NONE',  ( -34.42500000000001137, -22.22500000000000142, 5.000000000000000000 ) ) ;
#112978=FACE_OUTER_BOUND ( 'NONE', #13772, .T. ) ;
#112979=CARTESIAN_POINT ( 'NONE',  ( 3.473360963642126098, -5.240707523384232402, 16.25846745537496574 ) ) ;
#112980=ORIENTED_EDGE ( 'NONE', *, *, #101526, .F. ) ;
#112981=EDGE_CURVE ( 'NONE', #20866, #52318, #93865, .T. ) ;
#112983=EDGE_LOOP ( 'NONE', ( #38947, #49016, #113047, #37889 ) ) ;
#112984=ORIENTED_EDGE ( 'NONE', *, *, #111372, .F. ) ;
#112985=DIRECTION ( 'NONE',  ( -0.7071067811865486830, 0.7071067811865464625, -0.000000000000000000 ) ) ;
#112986=EDGE_LOOP ( 'NONE', ( #65866, #32110, #122792, #5004 ) ) ;
#112987=VECTOR ( 'NONE', #109643, 1000.000000000000000 ) ;
#112988=FACE_OUTER_BOUND ( 'NONE', #23225, .T. ) ;
#112989=DIRECTION ( 'NONE',  ( -0.7071067811865487940, 0.7071067811865463515, -0.000000000000000000 ) ) ;
#112990=EDGE_CURVE ( 'NONE', #71167, #139608, #40753, .T. ) ;
#112991=CARTESIAN_POINT ( 'NONE',  ( -15.06442625288296178, 7.619305877646137759, 4.652854425660915894 ) ) ;
#112994=DIRECTION ( 'NONE',  ( -0.7071067811865486830, -0.7071067811865464625, 0.000000000000000000 ) ) ;
#112995=ORIENTED_EDGE ( 'NONE', *, *, #111759, .T. ) ;
#112996=CARTESIAN_POINT ( 'NONE',  ( 51.18398860626899705, 28.73617430169823095, 5.000000000000000000 ) ) ;
#112998=ORIENTED_EDGE ( 'NONE', *, *, #73920, .T. ) ;
#113000=CARTESIAN_POINT ( 'NONE',  ( 0.000000000000000000, 0.000000000000000000, 5.000000000000000000 ) ) ;
#113001=ORIENTED_EDGE ( 'NONE', *, *, #72172, .F. ) ;
#113002=ORIENTED_EDGE ( 'NONE', *, *, #114830, .F. ) ;
#113003=ORIENTED_EDGE ( 'NONE', *, *, #95309, .F. ) ;
#113004=CARTESIAN_POINT ( 'NONE',  ( 4.499999999999976019, 13.08746187583911080, 4.000000000000000000 ) ) ;
#113005=FACE_OUTER_BOUND ( 'NONE', #107076, .T. ) ;
#113006=LINE ( 'NONE', #13675, #121471 ) ;
#113007=CARTESIAN_POINT ( 'NONE',  ( 5.999999999999955591, -18.03360074219755660, 5.000000000000000000 ) ) ;
#113008=ORIENTED_EDGE ( 'NONE', *, *, #119303, .T. ) ;
#113009=LINE ( 'NONE', #104257, #20758 ) ;
#113012=LINE ( 'NONE', #27421, #106713 ) ;
#113013=DIRECTION ( 'NONE',  ( 1.000000000000000000, 0.000000000000000000, 0.000000000000000000 ) ) ;
#113014=EDGE_LOOP ( 'NONE', ( #99358, #133375, #30812, #1118 ) ) ;
#113015=DIRECTION ( 'NONE',  ( 0.6830127018922180770, -0.6830127018922204085, -0.2588190451025213501 ) ) ;
#113016=ORIENTED_EDGE ( 'NONE', *, *, #71029, .T. ) ;
#113017=CARTESIAN_POINT ( 'NONE',  ( -36.18398860626899705, 28.73617430169812437, 5.000000000000000000 ) ) ;
#113018=ORIENTED_EDGE ( 'NONE', *, *, #122900, .T. ) ;
#113020=DIRECTION ( 'NONE',  ( -0.3543493200069162685, -0.000000000000000000, -0.9351131265310288487 ) ) ;
#113021=PLANE ( 'NONE',  #92368 ) ;
#113022=ORIENTED_EDGE ( 'NONE', *, *, #66125, .F. ) ;
#113023=CARTESIAN_POINT ( 'NONE',  ( -34.49999999999975131, 9.054329344830845727, 4.994342998332165884 ) ) ;
#113025=EDGE_LOOP ( 'NONE', ( #77556, #135378, #80539, #7827 ) ) ;
#113026=DIRECTION ( 'NONE',  ( -0.7071067811865486830, -0.7071067811865464625, 0.000000000000000000 ) ) ;
#113028=EDGE_CURVE ( 'NONE', #9322, #98313, #84958, .T. ) ;
#113029=LINE ( 'NONE', #13703, #13799 ) ;
#113030=VECTOR ( 'NONE', #22028, 1000.000000000000000 ) ;
#113031=DIRECTION ( 'NONE',  ( -0.000000000000000000, -0.3543493200069152693, 0.9351131265310292928 ) ) ;
#113032=EDGE_CURVE ( 'NONE', #42509, #69887, #15550, .T. ) ;
#113033=DIRECTION ( 'NONE',  ( 0.6830127018922181881, 0.6830127018922202975, -0.2588190451025214056 ) ) ;
#113034=DIRECTION ( 'NONE',  ( -0.000000000000000000, -0.3543493200069152693, 0.9351131265310292928 ) ) ;
#113036=EDGE_CURVE ( 'NONE', #51846, #39954, #107419, .T. ) ;
#113038=PLANE ( 'NONE',  #125460 ) ;
#113040=DIRECTION ( 'NONE',  ( -0.6830127018922181881, 0.6830127018922202975, -0.2588190451025214056 ) ) ;
#113041=CARTESIAN_POINT ( 'NONE',  ( -25.49999999999982236, -10.04351517176480613, -1.623559851933882081 ) ) ;
#113042=EDGE_CURVE ( 'NONE', #17152, #130600, #60571, .T. ) ;
#113043=ORIENTED_EDGE ( 'NONE', *, *, #38510, .T. ) ;
#113044=VERTEX_POINT ( 'NONE', #119687 ) ;
#113046=EDGE_LOOP ( 'NONE', ( #51625, #128279, #39043, #78409 ) ) ;
#113047=ORIENTED_EDGE ( 'NONE', *, *, #11363, .T. ) ;
#113048=AXIS2_PLACEMENT_3D ( 'NONE', #25457, #14600, #45131 ) ;
#113049=EDGE_LOOP ( 'NONE', ( #134574, #36867, #8737, #119918 ) ) ;
#113050=CARTESIAN_POINT ( 'NONE',  ( -25.62823445044369208, -8.240707523384207533, 11.38925528200758386 ) ) ;
#113051=DIRECTION ( 'NONE',  ( -1.000000000000000000, -1.424048422229243832E-14, 0.000000000000000000 ) ) ;
#113053=EDGE_LOOP ( 'NONE', ( #119852, #69657, #116944, #93586 ) ) ;
#113054=VECTOR ( 'NONE', #60078, 1000.000000000000000 ) ;
#113055=LINE ( 'NONE', #113787, #136572 ) ;
#113058=EDGE_CURVE ( 'NONE', #54027, #64418, #20388, .T. ) ;
#113059=PLANE ( 'NONE',  #34862 ) ;
#113060=CARTESIAN_POINT ( 'NONE',  ( -48.48921356237309510, -27.52281430457089328, 5.000000000000000000 ) ) ;
#113061=EDGE_CURVE ( 'NONE', #92120, #54748, #64631, .T. ) ;
#113062=VECTOR ( 'NONE', #30292, 999.9999999999998863 ) ;
#113063=DIRECTION ( 'NONE',  ( -0.000000000000000000, 0.000000000000000000, 1.000000000000000000 ) ) ;
#113064=CARTESIAN_POINT ( 'NONE',  ( 54.48921356237310221, -27.52281430457093236, 5.000000000000000000 ) ) ;
#113066=DIRECTION ( 'NONE',  ( -0.7071067811865486830, 0.7071067811865464625, 0.000000000000000000 ) ) ;
#113067=VECTOR ( 'NONE', #33336, 999.9999999999998863 ) ;
#113069=LINE ( 'NONE', #13739, #7664 ) ;
#113070=LINE ( 'NONE', #13740, #119482 ) ;
#113071=AXIS2_PLACEMENT_3D ( 'NONE', #129005, #84796, #84118 ) ;
#113072=PLANE ( 'NONE',  #29065 ) ;
#113073=EDGE_CURVE ( 'NONE', #5941, #50102, #30600, .T. ) ;
#113075=ORIENTED_EDGE ( 'NONE', *, *, #107656, .T. ) ;
#113076=VERTEX_POINT ( 'NONE', #8078 ) ;
#113078=EDGE_LOOP ( 'NONE', ( #96139, #52149, #95685, #105268 ) ) ;
#113079=PLANE ( 'NONE',  #3800 ) ;
#113080=EDGE_CURVE ( 'NONE', #17479, #11535, #129890, .T. ) ;
#113081=VECTOR ( 'NONE', #34966, 1000.000000000000000 ) ;
#113082=DIRECTION ( 'NONE',  ( 0.7071067811865486830, -0.7071067811865464625, -0.000000000000000000 ) ) ;
#113083=DIRECTION ( 'NONE',  ( 0.7071067811865487940, -0.7071067811865463515, 0.000000000000000000 ) ) ;
#113084=( BOUNDED_CURVE ( )  B_SPLINE_CURVE ( 3, ( #82987, #61283, #40222, #117706 ),
 .UNSPECIFIED., .F., .F. ) 
 B_SPLINE_CURVE_WITH_KNOTS ( ( 4, 4 ),
 ( 5.920967161967927161, 7.341195215986639155 ),
 .UNSPECIFIED. ) 
 CURVE ( )  GEOMETRIC_REPRESENTATION_ITEM ( )  RATIONAL_B_SPLINE_CURVE ( ( 1.000000000000000000, 0.8388583629366609395, 0.8388583629366609395, 1.000000000000000000 ) ) 
 REPRESENTATION_ITEM ( '' )  );
#113085=VECTOR ( 'NONE', #47146, 1000.000000000000114 ) ;
#113087=EDGE_LOOP ( 'NONE', ( #110973, #22218, #59839, #52309 ) ) ;
#113088=VERTEX_POINT ( 'NONE', #93159 ) ;
#113090=ADVANCED_FACE ( 'NONE', ( #53783 ), #19691, .T. ) ;
#113092=CARTESIAN_POINT ( 'NONE',  ( 34.42499999999998295, 21.72500000000000142, 0.000000000000000000 ) ) ;
#113093=( BOUNDED_CURVE ( )  B_SPLINE_CURVE ( 3, ( #42368, #26647, #140238, #119176 ),
 .UNSPECIFIED., .F., .T. ) 
 B_SPLINE_CURVE_WITH_KNOTS ( ( 4, 4 ),
 ( 4.350170835173027939, 4.500739107949208950 ),
 .UNSPECIFIED. ) 
 CURVE ( )  GEOMETRIC_REPRESENTATION_ITEM ( )  RATIONAL_B_SPLINE_CURVE ( ( 1.000000000000000000, 0.9981116584018958626, 0.9981116584018958626, 1.000000000000000000 ) ) 
 REPRESENTATION_ITEM ( '' )  );
#113094=VECTOR ( 'NONE', #31737, 1000.000000000000000 ) ;
#113096=EDGE_LOOP ( 'NONE', ( #25178, #127987, #1817, #24002 ) ) ;
#113097=ORIENTED_EDGE ( 'NONE', *, *, #5155, .F. ) ;
#113098=ORIENTED_EDGE ( 'NONE', *, *, #126985, .T. ) ;
#113099=DIRECTION ( 'NONE',  ( -0.3543493200069162685, -0.000000000000000000, -0.9351131265310288487 ) ) ;
#113101=ADVANCED_FACE ( 'NONE', ( #85652 ), #104743, .T. ) ;
#113103=VERTEX_POINT ( 'NONE', #63930 ) ;
#113104=ORIENTED_EDGE ( 'NONE', *, *, #16040, .F. ) ;
#113105=LINE ( 'NONE', #137748, #138135 ) ;
#113106=VERTEX_POINT ( 'NONE', #108101 ) ;
#113107=ORIENTED_EDGE ( 'NONE', *, *, #54500, .F. ) ;
#113108=VECTOR ( 'NONE', #4721, 1000.000000000000227 ) ;
#113109=ORIENTED_EDGE ( 'NONE', *, *, #122077, .F. ) ;
#113111=DIRECTION ( 'NONE',  ( -0.7071067811865486830, 0.7071067811865464625, 0.000000000000000000 ) ) ;
#113112=DIRECTION ( 'NONE',  ( -1.000000000000000000, -0.000000000000000000, -0.000000000000000000 ) ) ;
#113114=ORIENTED_EDGE ( 'NONE', *, *, #7950, .T. ) ;
#113115=LINE ( 'NONE', #70393, #69208 ) ;
#113117=CARTESIAN_POINT ( 'NONE',  ( 8.510786437626906675, -27.52281430457049183, 5.000000000000000000 ) ) ;
#113119=FACE_BOUND ( 'NONE', #17385, .T. ) ;
#113120=ORIENTED_EDGE ( 'NONE', *, *, #13172, .T. ) ;
#113122=FACE_OUTER_BOUND ( 'NONE', #1516, .T. ) ;
#113123=EDGE_CURVE ( 'NONE', #12722, #25035, #16271, .T. ) ;
#113124=FACE_OUTER_BOUND ( 'NONE', #129788, .T. ) ;
#113125=EDGE_LOOP ( 'NONE', ( #103387, #66098, #138812, #122181 ) ) ;
#113126=LINE ( 'NONE', #125457, #115209 ) ;
#113127=ORIENTED_EDGE ( 'NONE', *, *, #114540, .F. ) ;
#113129=VERTEX_POINT ( 'NONE', #9503 ) ;
#113132=LINE ( 'NONE', #2948, #78862 ) ;
#113133=DIRECTION ( 'NONE',  ( -0.7071067811865486830, -0.7071067811865464625, 0.000000000000000000 ) ) ;
#113134=ORIENTED_EDGE ( 'NONE', *, *, #41635, .F. ) ;
#113135=DIRECTION ( 'NONE',  ( -0.7071067811865486830, -0.7071067811865464625, 0.000000000000000000 ) ) ;
#113136=LINE ( 'NONE', #34906, #6209 ) ;
#113137=CARTESIAN_POINT ( 'NONE',  ( -12.29974487139158512, -27.71228299555214747, 4.000000000000000000 ) ) ;
#113138=EDGE_CURVE ( 'NONE', #114619, #36553, #97980, .T. ) ;
#113139=DIRECTION ( 'NONE',  ( -0.7071067811865486830, 0.7071067811865464625, 0.000000000000000000 ) ) ;
#113140=FACE_OUTER_BOUND ( 'NONE', #113280, .T. ) ;
#113141=ORIENTED_EDGE ( 'NONE', *, *, #43361, .T. ) ;
#113142=ORIENTED_EDGE ( 'NONE', *, *, #24351, .T. ) ;
#113143=EDGE_LOOP ( 'NONE', ( #35546, #9159, #284, #68947 ) ) ;
#113144=ORIENTED_EDGE ( 'NONE', *, *, #130272, .T. ) ;
#113145=PLANE ( 'NONE',  #49506 ) ;
#113146=VECTOR ( 'NONE', #88749, 1000.000000000000000 ) ;
#113147=AXIS2_PLACEMENT_3D ( 'NONE', #19940, #41710, #76503 ) ;
#113148=ORIENTED_EDGE ( 'NONE', *, *, #33201, .T. ) ;
#113149=VECTOR ( 'NONE', #23985, 1000.000000000000000 ) ;
#113151=VERTEX_POINT ( 'NONE', #21120 ) ;
#113152=PLANE ( 'NONE',  #87357 ) ;
#113153=EDGE_CURVE ( 'NONE', #63812, #37944, #2181, .T. ) ;
#113157=CARTESIAN_POINT ( 'NONE',  ( 21.29974487139158512, -27.71228299555221142, 4.000000000000000000 ) ) ;
#113158=VECTOR ( 'NONE', #52714, 1000.000000000000000 ) ;
#113159=VECTOR ( 'NONE', #95914, 1000.000000000000000 ) ;
#113160=ORIENTED_EDGE ( 'NONE', *, *, #122037, .T. ) ;
#113161=CARTESIAN_POINT ( 'NONE',  ( 22.49999999999984368, -1.695981523266237634, 4.571483868317931964 ) ) ;
#113164=ORIENTED_EDGE ( 'NONE', *, *, #65820, .F. ) ;
#113166=CARTESIAN_POINT ( 'NONE',  ( -9.299744871391588674, -27.71228299555212971, 4.000000000000000000 ) ) ;
#113167=DIRECTION ( 'NONE',  ( 0.7071067811865487940, -0.7071067811865463515, 0.000000000000000000 ) ) ;
#113169=CARTESIAN_POINT ( 'NONE',  ( -24.18398860626899705, 28.73617430169804265, 5.000000000000000000 ) ) ;
#113170=LINE ( 'NONE', #78429, #125923 ) ;
#113171=ORIENTED_EDGE ( 'NONE', *, *, #58883, .T. ) ;
#113172=VECTOR ( 'NONE', #26214, 1000.000000000000114 ) ;
#113173=FACE_OUTER_BOUND ( 'NONE', #94763, .T. ) ;
#113174=DIRECTION ( 'NONE',  ( 0.3543493200069162685, -0.000000000000000000, -0.9351131265310288487 ) ) ;
#113175=DIRECTION ( 'NONE',  ( -0.7071067811865486830, 0.7071067811865464625, 0.000000000000000000 ) ) ;
#113176=FACE_OUTER_BOUND ( 'NONE', #38452, .T. ) ;
#113178=EDGE_CURVE ( 'NONE', #9024, #83531, #36, .T. ) ;
#113179=ORIENTED_EDGE ( 'NONE', *, *, #77644, .F. ) ;
#113180=CARTESIAN_POINT ( 'NONE',  ( -26.99999999999980815, 16.55218569542899587, 5.000000000000000000 ) ) ;
#113181=VECTOR ( 'NONE', #96798, 999.9999999999998863 ) ;
#113182=CARTESIAN_POINT ( 'NONE',  ( 2.510786437626908008, -27.52281430457053446, 5.000000000000000000 ) ) ;
#113183=DIRECTION ( 'NONE',  ( 0.6830127018922181881, 0.6830127018922202975, -0.2588190451025214056 ) ) ;
#113185=VECTOR ( 'NONE', #54807, 1000.000000000000000 ) ;
#113186=LINE ( 'NONE', #13149, #49328 ) ;
#113187=AXIS2_PLACEMENT_3D ( 'NONE', #14077, #59765, #58377 ) ;
#113188=ORIENTED_EDGE ( 'NONE', *, *, #122873, .T. ) ;
#113190=CARTESIAN_POINT ( 'NONE',  ( -27.18398860626900060, 28.73617430169806042, 5.000000000000000000 ) ) ;
#113191=VERTEX_POINT ( 'NONE', #11641 ) ;
#113192=EDGE_LOOP ( 'NONE', ( #112163, #40613, #12000 ) ) ;
#113195=EDGE_LOOP ( 'NONE', ( #22426, #85584, #112611, #83703 ) ) ;
#113196=VECTOR ( 'NONE', #16682, 1000.000000000000000 ) ;
#113197=ADVANCED_FACE ( 'NONE', ( #46503 ), #87802, .T. ) ;
#113198=CARTESIAN_POINT ( 'NONE',  ( 32.29289321881323360, -6.740707523384209310, 5.000000000000000000 ) ) ;
#113199=EDGE_CURVE ( 'NONE', #78047, #50562, #78373, .T. ) ;
#113200=DIRECTION ( 'NONE',  ( 0.7071067811865487940, 0.7071067811865463515, -0.000000000000000000 ) ) ;
#113201=ORIENTED_EDGE ( 'NONE', *, *, #70637, .F. ) ;
#113203=CARTESIAN_POINT ( 'NONE',  ( -83.99451991528748351, 28.92564299267996830, 4.000000000000000000 ) ) ;
#113204=DIRECTION ( 'NONE',  ( 0.7071067811865486830, -0.7071067811865464625, -0.000000000000000000 ) ) ;
#113205=CARTESIAN_POINT ( 'NONE',  ( -23.00492477221180110, -5.240707523384232402, 12.38332538355501100 ) ) ;
#113206=VECTOR ( 'NONE', #108172, 1000.000000000000000 ) ;
#113207=DIRECTION ( 'NONE',  ( 0.6830127018922180770, -0.6830127018922204085, -0.2588190451025214056 ) ) ;
#113208=FACE_OUTER_BOUND ( 'NONE', #46047, .T. ) ;
#113209=DIRECTION ( 'NONE',  ( -0.000000000000000000, 0.3543493200069153248, 0.9351131265310292928 ) ) ;
#113210=PLANE ( 'NONE',  #133402 ) ;
#113211=ADVANCED_FACE ( 'NONE', ( #142905 ), #55195, .F. ) ;
#113212=VERTEX_POINT ( 'NONE', #79118 ) ;
#113214=ORIENTED_EDGE ( 'NONE', *, *, #104328, .T. ) ;
#113215=ORIENTED_EDGE ( 'NONE', *, *, #69240, .F. ) ;
#113217=ORIENTED_EDGE ( 'NONE', *, *, #10697, .T. ) ;
#113218=ORIENTED_EDGE ( 'NONE', *, *, #94378, .F. ) ;
#113219=VERTEX_POINT ( 'NONE', #47908 ) ;
#113221=DIRECTION ( 'NONE',  ( 2.781805975412906507E-17, 0.3543493200069153248, 0.9351131265310292928 ) ) ;
#113222=ORIENTED_EDGE ( 'NONE', *, *, #51762, .T. ) ;
#113223=CARTESIAN_POINT ( 'NONE',  ( 18.70710678118640757, -18.74070752338409562, 5.000000000000000000 ) ) ;
#113225=LINE ( 'NONE', #57460, #113512 ) ;
#113226=EDGE_CURVE ( 'NONE', #54347, #76671, #26829, .T. ) ;
#113227=CARTESIAN_POINT ( 'NONE',  ( 19.05000000000000071, 3.174999999999997158, 5.000000000000000000 ) ) ;
#113229=VERTEX_POINT ( 'NONE', #71078 ) ;
#113230=EDGE_CURVE ( 'NONE', #87384, #28061, #2932, .T. ) ;
#113231=LINE ( 'NONE', #58208, #122821 ) ;
#113232=DIRECTION ( 'NONE',  ( 0.7071067811865487940, -0.7071067811865463515, 0.000000000000000000 ) ) ;
#113233=DIRECTION ( 'NONE',  ( -0.000000000000000000, -0.3543493200069152693, 0.9351131265310292928 ) ) ;
#113234=CARTESIAN_POINT ( 'NONE',  ( 5.719980320105927163, 0.7592924766157069794, 14.27032725228010612 ) ) ;
#113235=LINE ( 'NONE', #3730, #79808 ) ;
#113237=CARTESIAN_POINT ( 'NONE',  ( 19.00193056682084247, -22.22500000000000142, 4.500000000000000888 ) ) ;
#113239=DIRECTION ( 'NONE',  ( 0.7071067811865487940, 0.7071067811865463515, 0.000000000000000000 ) ) ;
#113240=DIRECTION ( 'NONE',  ( -0.7071067811865486830, 0.7071067811865464625, 0.000000000000000000 ) ) ;
#113241=VERTEX_POINT ( 'NONE', #137758 ) ;
#113244=EDGE_CURVE ( 'NONE', #17447, #86210, #81969, .T. ) ;
#113245=ORIENTED_EDGE ( 'NONE', *, *, #124168, .F. ) ;
#113246=DIRECTION ( 'NONE',  ( -0.7071067811865486830, -0.7071067811865464625, -0.000000000000000000 ) ) ;
#113247=ORIENTED_EDGE ( 'NONE', *, *, #31216, .F. ) ;
#113248=EDGE_CURVE ( 'NONE', #133165, #60739, #82654, .T. ) ;
#113249=CARTESIAN_POINT ( 'NONE',  ( 0.000000000000000000, 0.000000000000000000, 5.000000000000000000 ) ) ;
#113250=DIRECTION ( 'NONE',  ( 0.7071067811865486830, -0.7071067811865464625, -0.000000000000000000 ) ) ;
#113253=LINE ( 'NONE', #58235, #117312 ) ;
#113254=ORIENTED_EDGE ( 'NONE', *, *, #79391, .T. ) ;
#113255=ADVANCED_FACE ( 'NONE', ( #113840 ), #92795, .F. ) ;
#113256=CARTESIAN_POINT ( 'NONE',  ( 31.49999999999979039, 5.696342897626542445, -7.587980461218329253 ) ) ;
#113258=VECTOR ( 'NONE', #37263, 1000.000000000000000 ) ;
#113260=CARTESIAN_POINT ( 'NONE',  ( 1.171830600776462061, 3.759292476615678336, 4.000000000000000000 ) ) ;
#113261=CARTESIAN_POINT ( 'NONE',  ( -60.18398860626900415, 28.73617430169829490, 5.000000000000000000 ) ) ;
#113262=VECTOR ( 'NONE', #66454, 1000.000000000000227 ) ;
#113264=EDGE_LOOP ( 'NONE', ( #107599, #67343, #114566, #72347 ) ) ;
#113265=CARTESIAN_POINT ( 'NONE',  ( 21.18398860626899349, 28.73617430169802134, 5.000000000000000000 ) ) ;
#113266=ORIENTED_EDGE ( 'NONE', *, *, #12563, .T. ) ;
#113267=CARTESIAN_POINT ( 'NONE',  ( -51.18398860626899705, 28.73617430169823095, 5.000000000000000000 ) ) ;
#113269=CARTESIAN_POINT ( 'NONE',  ( -42.18398860626899705, 28.73617430169816700, 5.000000000000000000 ) ) ;
#113270=ADVANCED_FACE ( 'NONE', ( #37735 ), #27528, .F. ) ;
#113271=EDGE_CURVE ( 'NONE', #36826, #134985, #115224, .T. ) ;
#113272=LINE ( 'NONE', #24847, #37097 ) ;
#113273=CARTESIAN_POINT ( 'NONE',  ( 12.00548008471251293, 28.92564299267929684, 4.000000000000000000 ) ) ;
#113274=AXIS2_PLACEMENT_3D ( 'NONE', #73300, #40666, #16755 ) ;
#113275=EDGE_CURVE ( 'NONE', #16581, #50105, #58081, .T. ) ;
#113276=CARTESIAN_POINT ( 'NONE',  ( 8.926082202452091607, -22.22500000000000142, -11.61681428604210353 ) ) ;
#113279=CARTESIAN_POINT ( 'NONE',  ( 19.49999999999987921, 22.08746187583901843, 4.000000000000000000 ) ) ;
#113280=EDGE_LOOP ( 'NONE', ( #67624, #99363, #76164, #105633 ) ) ;
#113281=ORIENTED_EDGE ( 'NONE', *, *, #56461, .F. ) ;
#113282=AXIS2_PLACEMENT_3D ( 'NONE', #43001, #87909, #32849 ) ;
#113283=DIRECTION ( 'NONE',  ( -0.000000000000000000, 0.3543493200069153248, 0.9351131265310292928 ) ) ;
#113286=FACE_OUTER_BOUND ( 'NONE', #142573, .T. ) ;
#113287=ORIENTED_EDGE ( 'NONE', *, *, #68604, .T. ) ;
#113289=VECTOR ( 'NONE', #107398, 1000.000000000000000 ) ;
#113290=VECTOR ( 'NONE', #20680, 999.9999999999998863 ) ;
#113291=VECTOR ( 'NONE', #74004, 1000.000000000000000 ) ;
#113292=FACE_BOUND ( 'NONE', #124979, .T. ) ;
#113293=CARTESIAN_POINT ( 'NONE',  ( -13.49999999999990052, -6.839392718269134974, -8.480912228396052299 ) ) ;
#113294=DIRECTION ( 'NONE',  ( -0.7071067811865486830, 0.7071067811865464625, 0.000000000000000000 ) ) ;
#113296=CARTESIAN_POINT ( 'NONE',  ( 2.816011393730999401, 28.73617430169785436, 5.000000000000000000 ) ) ;
#113297=ORIENTED_EDGE ( 'NONE', *, *, #108613, .F. ) ;
#113298=VECTOR ( 'NONE', #39638, 1000.000000000000114 ) ;
#113299=ORIENTED_EDGE ( 'NONE', *, *, #62263, .T. ) ;
#113301=LINE ( 'NONE', #3114, #63429 ) ;
#113302=ORIENTED_EDGE ( 'NONE', *, *, #134853, .F. ) ;
#113305=EDGE_LOOP ( 'NONE', ( #114448, #68976, #83749, #63076 ) ) ;
#113306=PLANE ( 'NONE',  #64996 ) ;
#113307=ADVANCED_FACE ( 'NONE', ( #81242 ), #71788, .F. ) ;
#113308=EDGE_LOOP ( 'NONE', ( #39470, #95060, #15661, #75876, #64954 ) ) ;
#113309=CARTESIAN_POINT ( 'NONE',  ( 22.17183060077632817, 21.75929247661549937, 4.000000000000000000 ) ) ;
#113312=PLANE ( 'NONE',  #47893 ) ;
#113314=CARTESIAN_POINT ( 'NONE',  ( 27.18398860626900060, 28.73617430169806042, 5.000000000000000000 ) ) ;
#113315=CARTESIAN_POINT ( 'NONE',  ( -17.20666063542140378, 21.75929247661549937, 4.998822639870711626 ) ) ;
#113316=LINE ( 'NONE', #24195, #93278 ) ;
#113317=CARTESIAN_POINT ( 'NONE',  ( -10.49999999999992184, 21.05218569542895679, 5.000000000000000000 ) ) ;
#113319=VERTEX_POINT ( 'NONE', #102281 ) ;
#113321=CARTESIAN_POINT ( 'NONE',  ( 20.29298673570680123, -21.74070752338406720, 4.999753212805221558 ) ) ;
#113322=ORIENTED_EDGE ( 'NONE', *, *, #4790, .F. ) ;
#113323=ORIENTED_EDGE ( 'NONE', *, *, #45365, .F. ) ;
#113324=ORIENTED_EDGE ( 'NONE', *, *, #142804, .T. ) ;
#113325=CARTESIAN_POINT ( 'NONE',  ( 11.67183060077638856, -9.740707523384186217, 4.000000000000000000 ) ) ;
#113326=EDGE_CURVE ( 'NONE', #91987, #48040, #115959, .T. ) ;
#113327=EDGE_CURVE ( 'NONE', #111735, #140719, #92075, .T. ) ;
#113328=DIRECTION ( 'NONE',  ( 0.7071067811865487940, 0.7071067811865463515, 0.000000000000000000 ) ) ;
#113329=ORIENTED_EDGE ( 'NONE', *, *, #30291, .T. ) ;
#113330=FACE_OUTER_BOUND ( 'NONE', #5558, .T. ) ;
#113334=ORIENTED_EDGE ( 'NONE', *, *, #40373, .T. ) ;
#113335=ADVANCED_FACE ( 'NONE', ( #135608 ), #80524, .T. ) ;
#113336=LINE ( 'NONE', #35838, #64275 ) ;
#113337=CARTESIAN_POINT ( 'NONE',  ( -23.99999999999983302, -6.108550654416979420, -3.114665004255023462 ) ) ;
#113338=DIRECTION ( 'NONE',  ( -0.7071067811865486830, 0.7071067811865464625, 0.000000000000000000 ) ) ;
#113340=ORIENTED_EDGE ( 'NONE', *, *, #138240, .T. ) ;
#113341=ORIENTED_EDGE ( 'NONE', *, *, #87182, .T. ) ;
#113342=CARTESIAN_POINT ( 'NONE',  ( -26.99999999999980815, -0.4125381241607481431, 4.000000000000000000 ) ) ;
#113343=LINE ( 'NONE', #14028, #40029 ) ;
#113344=DIRECTION ( 'NONE',  ( -0.7071067811865486830, -0.7071067811865464625, 0.000000000000000000 ) ) ;
#113345=EDGE_CURVE ( 'NONE', #107684, #118381, #36985, .T. ) ;
#113346=ORIENTED_EDGE ( 'NONE', *, *, #5662, .F. ) ;
#113350=CARTESIAN_POINT ( 'NONE',  ( 20.29289321881332242, -12.74070752338415247, 5.000000000000000000 ) ) ;
#113351=AXIS2_PLACEMENT_3D ( 'NONE', #37541, #39688, #83172 ) ;
#113352=ORIENTED_EDGE ( 'NONE', *, *, #24055, .T. ) ;
#113353=AXIS2_PLACEMENT_3D ( 'NONE', #41308, #30454, #53639 ) ;
#113354=ADVANCED_FACE ( 'NONE', ( #26131 ), #70394, .F. ) ;
#113355=VECTOR ( 'NONE', #11723, 1000.000000000000227 ) ;
#113356=AXIS2_PLACEMENT_3D ( 'NONE', #64429, #139164, #20185 ) ;
#113357=CARTESIAN_POINT ( 'NONE',  ( -32.99451991528749062, 28.92564299267960948, 4.000000000000000000 ) ) ;
#113358=CARTESIAN_POINT ( 'NONE',  ( -23.99451991528749062, 28.92564299267954908, 4.000000000000000000 ) ) ;
#113359=PLANE ( 'NONE',  #42388 ) ;
#113360=AXIS2_PLACEMENT_3D ( 'NONE', #31500, #130105, #56145 ) ;
#113361=CARTESIAN_POINT ( 'NONE',  ( -12.18398860626900060, 28.73617430169795739, 5.000000000000000000 ) ) ;
#113362=CARTESIAN_POINT ( 'NONE',  ( -34.92500000000001137, -21.72500000000000142, 5.000000000000000000 ) ) ;
#113363=ORIENTED_EDGE ( 'NONE', *, *, #1169, .F. ) ;
#113364=EDGE_LOOP ( 'NONE', ( #59184, #109772, #80657, #104197 ) ) ;
#113365=ADVANCED_FACE ( 'NONE', ( #28983 ), #73216, .T. ) ;
#113367=LINE ( 'NONE', #24243, #93337 ) ;
#113368=CARTESIAN_POINT ( 'NONE',  ( -34.75611968250421313, -3.187065745292602781, 4.955485411084894487 ) ) ;
#113369=AXIS2_PLACEMENT_3D ( 'NONE', #27070, #73454, #6703 ) ;
#113370=CARTESIAN_POINT ( 'NONE',  ( 4.499999999999968914, -4.796895815301017052, -3.611700055028670864 ) ) ;
#113371=LINE ( 'NONE', #70644, #25095 ) ;
#113372=PLANE ( 'NONE',  #74564 ) ;
#113373=ORIENTED_EDGE ( 'NONE', *, *, #126342, .T. ) ;
#113374=EDGE_CURVE ( 'NONE', #99040, #98806, #52153, .T. ) ;
#113375=CARTESIAN_POINT ( 'NONE',  ( 26.51078643762690845, -27.52281430457036748, 5.000000000000000000 ) ) ;
#113376=VECTOR ( 'NONE', #53122, 1000.000000000000000 ) ;
#113378=FACE_OUTER_BOUND ( 'NONE', #83468, .T. ) ;
#113381=EDGE_CURVE ( 'NONE', #119254, #93631, #9313, .T. ) ;
#113382=EDGE_CURVE ( 'NONE', #2974, #104604, #118085, .T. ) ;
#113384=LINE ( 'NONE', #93792, #11657 ) ;
#113386=FACE_OUTER_BOUND ( 'NONE', #87656, .T. ) ;
#113387=ORIENTED_EDGE ( 'NONE', *, *, #13323, .F. ) ;
#113388=LINE ( 'NONE', #24262, #75591 ) ;
#113389=VECTOR ( 'NONE', #85988, 1000.000000000000000 ) ;
#113390=ADVANCED_FACE ( 'NONE', ( #127579 ), #141296, .F. ) ;
#113391=VECTOR ( 'NONE', #117305, 1000.000000000000000 ) ;
#113393=DIRECTION ( 'NONE',  ( -0.7071067811865486830, 0.7071067811865464625, 0.000000000000000000 ) ) ;
#113394=PLANE ( 'NONE',  #25361 ) ;
#113395=EDGE_CURVE ( 'NONE', #87783, #135817, #138461, .T. ) ;
#113396=CARTESIAN_POINT ( 'NONE',  ( 17.21837311707493612, 21.74787736706806029, 4.999607392498049308 ) ) ;
#113397=PLANE ( 'NONE',  #40752 ) ;
#113398=VECTOR ( 'NONE', #66111, 1000.000000000000000 ) ;
#113400=CIRCLE ( 'NONE', #118028, 0.5000000000000004441 ) ;
#113402=VERTEX_POINT ( 'NONE', #31138 ) ;
#113403=DIRECTION ( 'NONE',  ( 0.7071067811865486830, -0.7071067811865464625, -0.000000000000000000 ) ) ;
#113406=CARTESIAN_POINT ( 'NONE',  ( -1.499999999999984013, 12.43112307739206024, 4.000000000000000000 ) ) ;
#113407=PLANE ( 'NONE',  #136029 ) ;
#113409=CARTESIAN_POINT ( 'NONE',  ( 4.499999999999968914, -5.947814304570774091, 5.000000000000000000 ) ) ;
#113410=LINE ( 'NONE', #2488, #4262 ) ;
#113411=ORIENTED_EDGE ( 'NONE', *, *, #33473, .T. ) ;
#113413=ADVANCED_FACE ( 'NONE', ( #106496 ), #128993, .T. ) ;
#113414=DIRECTION ( 'NONE',  ( -0.000000000000000000, 0.000000000000000000, 1.000000000000000000 ) ) ;
#113415=CARTESIAN_POINT ( 'NONE',  ( 35.99451991528749772, 28.92564299267963079, 4.000000000000000000 ) ) ;
#113416=CARTESIAN_POINT ( 'NONE',  ( -0.4892135623730947680, -27.52281430457055578, 5.000000000000000000 ) ) ;
#113418=EDGE_LOOP ( 'NONE', ( #26960, #32036, #7038, #48383 ) ) ;
#113419=EDGE_CURVE ( 'NONE', #22931, #129409, #75353, .T. ) ;
#113420=DIRECTION ( 'NONE',  ( -0.6830127018922180770, -0.6830127018922204085, -0.2588190451025213501 ) ) ;
#113421=CARTESIAN_POINT ( 'NONE',  ( -31.49999999999977263, 22.08746187583901843, 4.000000000000000000 ) ) ;
#113423=CARTESIAN_POINT ( 'NONE',  ( 6.707106781186501721, 8.259292476615629042, 5.000000000000000000 ) ) ;
#113424=ORIENTED_EDGE ( 'NONE', *, *, #39229, .F. ) ;
#113425=VERTEX_POINT ( 'NONE', #74645 ) ;
#113426=VECTOR ( 'NONE', #25615, 1000.000000000000227 ) ;
#113427=DIRECTION ( 'NONE',  ( -0.000000000000000000, -0.3543493200069152693, 0.9351131265310292928 ) ) ;
#113429=DIRECTION ( 'NONE',  ( 0.6830127018922180770, -0.6830127018922204085, -0.2588190451025213501 ) ) ;
#113430=DIRECTION ( 'NONE',  ( 0.7071067811865487940, 0.7071067811865463515, 0.000000000000000000 ) ) ;
#113431=ORIENTED_EDGE ( 'NONE', *, *, #137442, .F. ) ;
#113432=DIRECTION ( 'NONE',  ( 0.7071067811865487940, -0.7071067811865463515, 0.000000000000000000 ) ) ;
#113433=FACE_OUTER_BOUND ( 'NONE', #115196, .T. ) ;
#113434=DIRECTION ( 'NONE',  ( 0.7071067811865486830, -0.7071067811865464625, -0.000000000000000000 ) ) ;
#113436=LINE ( 'NONE', #68550, #122464 ) ;
#113438=ORIENTED_EDGE ( 'NONE', *, *, #106727, .T. ) ;
#113439=EDGE_CURVE ( 'NONE', #54392, #2047, #61635, .T. ) ;
#113440=VERTEX_POINT ( 'NONE', #73911 ) ;
#113442=EDGE_CURVE ( 'NONE', #118295, #16746, #128306, .T. ) ;
#113443=ORIENTED_EDGE ( 'NONE', *, *, #45032, .F. ) ;
#113444=CARTESIAN_POINT ( 'NONE',  ( 0.9950752277880503538, -5.240707523384228850, 12.38332538355495949 ) ) ;
#113449=ORIENTED_EDGE ( 'NONE', *, *, #37689, .F. ) ;
#113450=DIRECTION ( 'NONE',  ( 0.7071067811865487940, -0.7071067811865463515, 0.000000000000000000 ) ) ;
#113453=ORIENTED_EDGE ( 'NONE', *, *, #101338, .F. ) ;
#113454=DIRECTION ( 'NONE',  ( -0.7071067811865487940, 0.7071067811865463515, -0.000000000000000000 ) ) ;
#113455=ORIENTED_EDGE ( 'NONE', *, *, #67194, .F. ) ;
#113456=CARTESIAN_POINT ( 'NONE',  ( 15.00548008471250228, 28.92564299267927552, 4.000000000000000000 ) ) ;
#113457=PLANE ( 'NONE',  #139652 ) ;
#113459=AXIS2_PLACEMENT_3D ( 'NONE', #125527, #46583, #80600 ) ;
#113461=EDGE_LOOP ( 'NONE', ( #141481, #114436, #140920 ) ) ;
#113463=FACE_BOUND ( 'NONE', #70381, .T. ) ;
#113465=CARTESIAN_POINT ( 'NONE',  ( 54.48921356237310221, -27.52281430457093236, 5.000000000000000000 ) ) ;
#113467=VECTOR ( 'NONE', #14975, 1000.000000000000000 ) ;
#113468=DIRECTION ( 'NONE',  ( -0.7071067811865486830, -0.7071067811865464625, 0.000000000000000000 ) ) ;
#113471=ORIENTED_EDGE ( 'NONE', *, *, #98639, .F. ) ;
#113472=ORIENTED_EDGE ( 'NONE', *, *, #126864, .T. ) ;
#113474=ORIENTED_EDGE ( 'NONE', *, *, #124037, .T. ) ;
#113476=VERTEX_POINT ( 'NONE', #139194 ) ;
#113477=VECTOR ( 'NONE', #37673, 1000.000000000000000 ) ;
#113478=DIRECTION ( 'NONE',  ( -0.7071067811865487940, 0.7071067811865463515, 0.000000000000000000 ) ) ;
#113480=DIRECTION ( 'NONE',  ( -0.6830127018922180770, -0.6830127018922204085, -0.2588190451025213501 ) ) ;
#113481=ORIENTED_EDGE ( 'NONE', *, *, #59376, .T. ) ;
#113482=DIRECTION ( 'NONE',  ( 0.7071067811865487940, 0.7071067811865463515, -0.000000000000000000 ) ) ;
#113483=DIRECTION ( 'NONE',  ( -0.7071067811865487940, 0.7071067811865463515, 0.000000000000000000 ) ) ;
#113484=LINE ( 'NONE', #91743, #13373 ) ;
#113485=CARTESIAN_POINT ( 'NONE',  ( 35.99451991528749772, 28.92564299267963079, 4.000000000000000000 ) ) ;
#113486=VECTOR ( 'NONE', #23553, 1000.000000000000000 ) ;
#113487=PLANE ( 'NONE',  #41544 ) ;
#113488=DIRECTION ( 'NONE',  ( 1.000000000000000000, 0.000000000000000000, 0.000000000000000000 ) ) ;
#113490=VECTOR ( 'NONE', #60884, 1000.000000000000227 ) ;
#113491=DIRECTION ( 'NONE',  ( -0.7071067811865486830, -0.7071067811865464625, -0.000000000000000000 ) ) ;
#113492=CARTESIAN_POINT ( 'NONE',  ( -34.92500000000001137, -12.53194198458142061, -8.170704600677588303 ) ) ;
#113494=VERTEX_POINT ( 'NONE', #119517 ) ;
#113495=EDGE_LOOP ( 'NONE', ( #18265, #22509, #70156, #27666 ) ) ;
#113496=EDGE_CURVE ( 'NONE', #129679, #105081, #20212, .T. ) ;
#113497=EDGE_CURVE ( 'NONE', #22057, #92143, #51458, .T. ) ;
#113501=ORIENTED_EDGE ( 'NONE', *, *, #68484, .T. ) ;
#113502=ADVANCED_FACE ( 'NONE', ( #18796 ), #107241, .F. ) ;
#113503=EDGE_CURVE ( 'NONE', #81462, #134437, #132606, .T. ) ;
#113507=FACE_OUTER_BOUND ( 'NONE', #33792, .T. ) ;
#113509=EDGE_CURVE ( 'NONE', #751, #67859, #65204, .T. ) ;
#113510=CARTESIAN_POINT ( 'NONE',  ( 11.87852683662845799, -20.24070752338407431, 7.412974875817763376 ) ) ;
#113512=VECTOR ( 'NONE', #113954, 1000.000000000000000 ) ;
#113516=CARTESIAN_POINT ( 'NONE',  ( -8.671830600776399223, -21.74070752338405299, 4.000000000000000000 ) ) ;
#113517=DIRECTION ( 'NONE',  ( -0.000000000000000000, 0.3543493200069153248, 0.9351131265310292928 ) ) ;
#113519=ORIENTED_EDGE ( 'NONE', *, *, #81995, .F. ) ;
#113520=CARTESIAN_POINT ( 'NONE',  ( -56.99451991528749062, 28.92564299267978001, 4.000000000000000000 ) ) ;
#113521=ORIENTED_EDGE ( 'NONE', *, *, #99401, .T. ) ;
#113522=ORIENTED_EDGE ( 'NONE', *, *, #10741, .F. ) ;
#113524=LINE ( 'NONE', #36680, #72609 ) ;
#113526=LINE ( 'NONE', #27231, #118665 ) ;
#113527=DIRECTION ( 'NONE',  ( -0.3543493200069163240, -0.000000000000000000, 0.9351131265310288487 ) ) ;
#113528=DIRECTION ( 'NONE',  ( 0.6830127018922181881, 0.6830127018922202975, -0.2588190451025214056 ) ) ;
#113529=PLANE ( 'NONE',  #32637 ) ;
#113530=EDGE_LOOP ( 'NONE', ( #111642, #61289, #141404, #128556 ) ) ;
#113531=EDGE_CURVE ( 'NONE', #119333, #24024, #34701, .T. ) ;
#113532=CIRCLE ( 'NONE', #136718, 5.968999999999998529 ) ;
#113533=CARTESIAN_POINT ( 'NONE',  ( 14.59122188827396549, 7.143407583703162089, 5.000000000000000000 ) ) ;
#113535=DIRECTION ( 'NONE',  ( -0.000000000000000000, 0.000000000000000000, 1.000000000000000000 ) ) ;
#113536=CARTESIAN_POINT ( 'NONE',  ( 1.499999999999990896, 9.431123077392093990, 4.000000000000000000 ) ) ;
#113537=CARTESIAN_POINT ( 'NONE',  ( -23.99451991528749062, 28.92564299267954908, 4.000000000000000000 ) ) ;
#113539=ORIENTED_EDGE ( 'NONE', *, *, #106436, .F. ) ;
#113540=ADVANCED_FACE ( 'NONE', ( #42736 ), #87639, .T. ) ;
#113541=ORIENTED_EDGE ( 'NONE', *, *, #127231, .F. ) ;
#113542=LINE ( 'NONE', #136021, #115748 ) ;
#113543=CARTESIAN_POINT ( 'NONE',  ( -42.48921356237308800, -27.52281430457085065, 5.000000000000000000 ) ) ;
#113544=CARTESIAN_POINT ( 'NONE',  ( -32.99451991528749062, 28.92564299267960948, 4.000000000000000000 ) ) ;
#113545=VECTOR ( 'NONE', #104474, 999.9999999999998863 ) ;
#113546=CARTESIAN_POINT ( 'NONE',  ( -9.792893218813386369, 15.75929247661555976, 5.000000000000000000 ) ) ;
#113548=VECTOR ( 'NONE', #116535, 999.9999999999998863 ) ;
#113549=EDGE_CURVE ( 'NONE', #132281, #63434, #10067, .T. ) ;
#113550=AXIS2_PLACEMENT_3D ( 'NONE', #116315, #6793, #95270 ) ;
#113551=CARTESIAN_POINT ( 'NONE',  ( 29.99999999999979394, -0.4125381241607516403, 4.000000000000000000 ) ) ;
#113552=DIRECTION ( 'NONE',  ( 0.7071067811865486830, -0.7071067811865464625, -0.000000000000000000 ) ) ;
#113553=DIRECTION ( 'NONE',  ( 0.7071067811865487940, 0.7071067811865463515, 0.000000000000000000 ) ) ;
#113555=ADVANCED_FACE ( 'NONE', ( #55030 ), #65924, .T. ) ;
#113556=FACE_OUTER_BOUND ( 'NONE', #36642, .T. ) ;
#113557=ORIENTED_EDGE ( 'NONE', *, *, #139235, .T. ) ;
#113558=AXIS2_PLACEMENT_3D ( 'NONE', #32074, #76304, #108880 ) ;
#113560=VECTOR ( 'NONE', #107131, 1000.000000000000000 ) ;
#113562=ORIENTED_EDGE ( 'NONE', *, *, #43585, .F. ) ;
#113564=AXIS2_PLACEMENT_3D ( 'NONE', #63469, #96043, #51861 ) ;
#113565=DIRECTION ( 'NONE',  ( -0.7071067811865486830, -0.7071067811865464625, 0.000000000000000000 ) ) ;
#113566=PLANE ( 'NONE',  #14001 ) ;
#113568=FACE_OUTER_BOUND ( 'NONE', #11934, .T. ) ;
#113569=CARTESIAN_POINT ( 'NONE',  ( 10.17183060077640100, -11.24070752338417201, 4.000000000000000000 ) ) ;
#113570=VERTEX_POINT ( 'NONE', #100671 ) ;
#113571=LINE ( 'NONE', #40846, #9027 ) ;
#113572=VERTEX_POINT ( 'NONE', #76800 ) ;
#113573=AXIS2_PLACEMENT_3D ( 'NONE', #130388, #75298, #63711 ) ;
#113574=ORIENTED_EDGE ( 'NONE', *, *, #119837, .F. ) ;
#113575=DIRECTION ( 'NONE',  ( -0.7071067811865487940, 0.7071067811865463515, -0.000000000000000000 ) ) ;
#113578=DIRECTION ( 'NONE',  ( -0.6830127018922180770, -0.6830127018922204085, -0.2588190451025213501 ) ) ;
#113579=ORIENTED_EDGE ( 'NONE', *, *, #17910, .T. ) ;
#113580=ADVANCED_FACE ( 'NONE', ( #10761 ), #86936, .F. ) ;
#113581=DIRECTION ( 'NONE',  ( -0.3543493200069162685, -0.000000000000000000, -0.9351131265310288487 ) ) ;
#113582=DIRECTION ( 'NONE',  ( 0.7071067811865487940, 0.7071067811865463515, 0.000000000000000000 ) ) ;
#113583=DIRECTION ( 'NONE',  ( 0.7071067811865487940, -0.7071067811865463515, 0.000000000000000000 ) ) ;
#113585=DIRECTION ( 'NONE',  ( -0.3543493200069162685, -0.000000000000000000, -0.9351131265310288487 ) ) ;
#113586=VECTOR ( 'NONE', #123032, 1000.000000000000000 ) ;
#113587=PLANE ( 'NONE',  #48954 ) ;
#113588=FACE_OUTER_BOUND ( 'NONE', #12740, .T. ) ;
#113590=AXIS2_PLACEMENT_3D ( 'NONE', #124153, #24838, #132927 ) ;
#113591=CARTESIAN_POINT ( 'NONE',  ( 23.99999999999983302, -21.03360074219752462, 5.000000000000000000 ) ) ;
#113592=ORIENTED_EDGE ( 'NONE', *, *, #139333, .F. ) ;
#113593=ADVANCED_FACE ( 'NONE', ( #31832 ), #109389, .T. ) ;
#113595=AXIS2_PLACEMENT_3D ( 'NONE', #69785, #58929, #13190 ) ;
#113596=DIRECTION ( 'NONE',  ( 0.7071067811865487940, -0.7071067811865463515, 0.000000000000000000 ) ) ;
#113597=CARTESIAN_POINT ( 'NONE',  ( 39.48921356237310221, -27.52281430457082934, 5.000000000000000000 ) ) ;
#113598=CARTESIAN_POINT ( 'NONE',  ( 0.7586007421979610310, 21.72500000000000853, 5.000000000000000000 ) ) ;
#113599=DIRECTION ( 'NONE',  ( 1.000000000000000000, 0.000000000000000000, 0.000000000000000000 ) ) ;
#113600=ORIENTED_EDGE ( 'NONE', *, *, #115263, .T. ) ;
#113601=VECTOR ( 'NONE', #1041, 1000.000000000000227 ) ;
#113602=LINE ( 'NONE', #47690, #23383 ) ;
#113603=CARTESIAN_POINT ( 'NONE',  ( -23.99451991528749062, 28.92564299267954908, 4.000000000000000000 ) ) ;
#113604=EDGE_CURVE ( 'NONE', #14564, #101438, #12207, .T. ) ;
#113605=ORIENTED_EDGE ( 'NONE', *, *, #417, .T. ) ;
#113606=CARTESIAN_POINT ( 'NONE',  ( -29.99999999999978328, -10.44781430457071991, 5.000000000000000000 ) ) ;
#113607=VECTOR ( 'NONE', #24252, 999.9999999999998863 ) ;
#113608=DIRECTION ( 'NONE',  ( 0.7071067811865486830, -0.7071067811865464625, -0.000000000000000000 ) ) ;
#113610=DIRECTION ( 'NONE',  ( 0.7071067811865487940, 0.7071067811865463515, 0.000000000000000000 ) ) ;
#113615=DIRECTION ( 'NONE',  ( -0.7071067811865486830, -0.7071067811865464625, 0.000000000000000000 ) ) ;
#113616=ORIENTED_EDGE ( 'NONE', *, *, #46140, .F. ) ;
#113618=ORIENTED_EDGE ( 'NONE', *, *, #93006, .T. ) ;
#113620=AXIS2_PLACEMENT_3D ( 'NONE', #52590, #62784, #43168 ) ;
#113621=EDGE_LOOP ( 'NONE', ( #81798, #40088, #126349, #126667 ) ) ;
#113625=LINE ( 'NONE', #75488, #27186 ) ;
#113626=LINE ( 'NONE', #14317, #17939 ) ;
#113628=DIRECTION ( 'NONE',  ( -0.000000000000000000, 0.000000000000000000, 1.000000000000000000 ) ) ;
#113629=DIRECTION ( 'NONE',  ( -0.7071067811865486830, -0.7071067811865464625, 0.000000000000000000 ) ) ;
#113630=EDGE_CURVE ( 'NONE', #46380, #50635, #121673, .T. ) ;
#113631=DIRECTION ( 'NONE',  ( 0.7071067811865487940, 0.7071067811865463515, -0.000000000000000000 ) ) ;
#113633=EDGE_CURVE ( 'NONE', #44164, #92497, #131869, .T. ) ;
#113634=VERTEX_POINT ( 'NONE', #120224 ) ;
#113635=CARTESIAN_POINT ( 'NONE',  ( 15.71462683630238111, 8.126010640810376273, 4.668119888204643075 ) ) ;
#113636=DIRECTION ( 'NONE',  ( 0.7071067811865487940, 0.7071067811865463515, -0.000000000000000000 ) ) ;
#113639=ORIENTED_EDGE ( 'NONE', *, *, #22089, .F. ) ;
#113642=ADVANCED_FACE ( 'NONE', ( #20938 ), #120970, .F. ) ;
#113643=CARTESIAN_POINT ( 'NONE',  ( 11.20710678118647152, 9.759292476615614831, 5.000000000000000000 ) ) ;
#113646=CARTESIAN_POINT ( 'NONE',  ( 30.29974487139158867, -27.71228299555227537, 4.000000000000000000 ) ) ;
#113647=CARTESIAN_POINT ( 'NONE',  ( -10.49999999999992539, -20.56887692260760758, 4.000000000000000000 ) ) ;
#113648=CARTESIAN_POINT ( 'NONE',  ( 63.48921356237309510, -27.52281430457099631, 5.000000000000000000 ) ) ;
#113653=CARTESIAN_POINT ( 'NONE',  ( 39.29974487139159578, -27.71228299555233576, 4.000000000000000000 ) ) ;
#113655=EDGE_LOOP ( 'NONE', ( #67186, #69620, #24698, #139795 ) ) ;
#113656=AXIS2_PLACEMENT_3D ( 'NONE', #126891, #72595, #4350 ) ;
#113658=VECTOR ( 'NONE', #71965, 1000.000000000000000 ) ;
#113659=CARTESIAN_POINT ( 'NONE',  ( 0.000000000000000000, 0.000000000000000000, 5.000000000000000000 ) ) ;
#113660=ORIENTED_EDGE ( 'NONE', *, *, #30153, .T. ) ;
#113661=FACE_OUTER_BOUND ( 'NONE', #142487, .T. ) ;
#113662=LINE ( 'NONE', #102093, #93490 ) ;
#113663=DIRECTION ( 'NONE',  ( -0.3543493200069162685, -0.000000000000000000, -0.9351131265310288487 ) ) ;
#113664=LINE ( 'NONE', #25226, #129503 ) ;
#113665=VECTOR ( 'NONE', #63994, 999.9999999999998863 ) ;
#113666=VECTOR ( 'NONE', #107523, 1000.000000000000227 ) ;
#113668=CARTESIAN_POINT ( 'NONE',  ( 60.18398860626900415, 28.73617430169829490, 5.000000000000000000 ) ) ;
#113669=ORIENTED_EDGE ( 'NONE', *, *, #128368, .T. ) ;
#113670=VECTOR ( 'NONE', #62560, 999.9999999999998863 ) ;
#113671=CARTESIAN_POINT ( 'NONE',  ( -23.70025512860841133, -27.71228299555189523, 4.000000000000000000 ) ) ;
#113672=CARTESIAN_POINT ( 'NONE',  ( 20.99999999999985434, -4.447814304570781196, 5.000000000000000000 ) ) ;
#113674=LINE ( 'NONE', #121678, #45751 ) ;
#113675=EDGE_LOOP ( 'NONE', ( #33199, #102360, #86089, #24801 ) ) ;
#113676=EDGE_CURVE ( 'NONE', #23262, #105676, #110786, .T. ) ;
#113677=ORIENTED_EDGE ( 'NONE', *, *, #27864, .F. ) ;
#113678=DIRECTION ( 'NONE',  ( -0.7071067811865486830, -0.7071067811865464625, 0.000000000000000000 ) ) ;
#113679=ORIENTED_EDGE ( 'NONE', *, *, #16404, .F. ) ;
#113680=ORIENTED_EDGE ( 'NONE', *, *, #135005, .F. ) ;
#113681=VECTOR ( 'NONE', #76563, 1000.000000000000000 ) ;
#113683=ORIENTED_EDGE ( 'NONE', *, *, #99940, .T. ) ;
#113685=ADVANCED_FACE ( 'NONE', ( #125994 ), #112953, .F. ) ;
#113686=DIRECTION ( 'NONE',  ( 0.7071067811865486830, -0.7071067811865464625, -0.000000000000000000 ) ) ;
#113687=PLANE ( 'NONE',  #142201 ) ;
#113688=ADVANCED_FACE ( 'NONE', ( #126672 ), #68773, .F. ) ;
#113690=DIRECTION ( 'NONE',  ( -0.7071067811865486830, 0.7071067811865464625, 0.000000000000000000 ) ) ;
#113692=EDGE_CURVE ( 'NONE', #13774, #124390, #127937, .T. ) ;
#113693=LINE ( 'NONE', #12936, #117640 ) ;
#113694=DIRECTION ( 'NONE',  ( 0.6830127018922181881, 0.6830127018922202975, -0.2588190451025214056 ) ) ;
#113695=VECTOR ( 'NONE', #117476, 1000.000000000000000 ) ;
#113696=LINE ( 'NONE', #14388, #11615 ) ;
#113697=EDGE_CURVE ( 'NONE', #20428, #114476, #81795, .T. ) ;
#113701=ADVANCED_FACE ( 'NONE', ( #3457 ), #36819, .T. ) ;
#113702=ORIENTED_EDGE ( 'NONE', *, *, #87479, .F. ) ;
#113703=AXIS2_PLACEMENT_3D ( 'NONE', #108236, #53935, #98130 ) ;
#113704=LINE ( 'NONE', #134043, #36496 ) ;
#113705=PLANE ( 'NONE',  #124067 ) ;
#113706=EDGE_LOOP ( 'NONE', ( #104559, #86688, #119092 ) ) ;
#113707=VECTOR ( 'NONE', #50579, 1000.000000000000227 ) ;
#113708=EDGE_LOOP ( 'NONE', ( #60064, #41321, #29806, #98292 ) ) ;
#113709=CARTESIAN_POINT ( 'NONE',  ( 27.32816939922334143, -21.74070752338406365, 4.000000000000000000 ) ) ;
#113710=EDGE_LOOP ( 'NONE', ( #81255, #22478, #55413, #58391 ) ) ;
#113712=PLANE ( 'NONE',  #69984 ) ;
#113713=DIRECTION ( 'NONE',  ( 1.000000000000000000, 0.000000000000000000, 0.000000000000000000 ) ) ;
#113715=VECTOR ( 'NONE', #52931, 1000.000000000000114 ) ;
#113717=DIRECTION ( 'NONE',  ( 0.7071067811865487940, 0.7071067811865463515, 0.000000000000000000 ) ) ;
#113718=ORIENTED_EDGE ( 'NONE', *, *, #13265, .T. ) ;
#113720=ORIENTED_EDGE ( 'NONE', *, *, #14577, .F. ) ;
#113721=ADVANCED_FACE ( 'NONE', ( #114384 ), #115061, .F. ) ;
#113722=CARTESIAN_POINT ( 'NONE',  ( -24.79289321881328334, 0.7592924766157104211, 5.000000000000000000 ) ) ;
#113723=VECTOR ( 'NONE', #130978, 1000.000000000000000 ) ;
#113726=CARTESIAN_POINT ( 'NONE',  ( -31.49999999999976552, 16.08746187583907528, 4.000000000000000000 ) ) ;
#113727=DIRECTION ( 'NONE',  ( -0.7071067811865487940, 0.7071067811865463515, 0.000000000000000000 ) ) ;
#113728=ORIENTED_EDGE ( 'NONE', *, *, #3860, .T. ) ;
#113729=VERTEX_POINT ( 'NONE', #124553 ) ;
#113730=VECTOR ( 'NONE', #57130, 999.9999999999998863 ) ;
#113731=EDGE_LOOP ( 'NONE', ( #116992, #58552, #99749, #81482 ) ) ;
#113732=LINE ( 'NONE', #12971, #38012 ) ;
#113733=LINE ( 'NONE', #17270, #88134 ) ;
#113734=DIRECTION ( 'NONE',  ( -0.3543493200069162685, -0.000000000000000000, -0.9351131265310288487 ) ) ;
#113735=VECTOR ( 'NONE', #120124, 1000.000000000000000 ) ;
#113736=CARTESIAN_POINT ( 'NONE',  ( -13.49999999999990763, 16.18958161055401490, -11.56426086740814441 ) ) ;
#113738=LINE ( 'NONE', #71670, #78628 ) ;
#113739=CARTESIAN_POINT ( 'NONE',  ( -23.99999999999982947, 20.70535890316559247, 1.956823837851970449 ) ) ;
#113740=DIRECTION ( 'NONE',  ( 0.7071067811865487940, 0.7071067811865463515, 0.000000000000000000 ) ) ;
#113741=CARTESIAN_POINT ( 'NONE',  ( 39.18398860626899705, 28.73617430169814568, 5.000000000000000000 ) ) ;
#113742=EDGE_CURVE ( 'NONE', #77649, #14760, #25956, .T. ) ;
#113743=EDGE_LOOP ( 'NONE', ( #67862, #112109, #114561, #89428 ) ) ;
#113744=VECTOR ( 'NONE', #55096, 1000.000000000000000 ) ;
#113745=CARTESIAN_POINT ( 'NONE',  ( -28.82816939922332367, -11.24070752338416845, 4.000000000000000000 ) ) ;
#113747=EDGE_CURVE ( 'NONE', #99063, #49422, #46321, .T. ) ;
#113748=CARTESIAN_POINT ( 'NONE',  ( -31.49999999999977973, -16.91253812416059077, 4.000000000000000000 ) ) ;
#113749=VERTEX_POINT ( 'NONE', #48414 ) ;
#113750=ORIENTED_EDGE ( 'NONE', *, *, #14513, .F. ) ;
#113751=DIRECTION ( 'NONE',  ( -0.3543493200069162685, -0.000000000000000000, -0.9351131265310288487 ) ) ;
#113752=FACE_OUTER_BOUND ( 'NONE', #50532, .T. ) ;
#113753=VECTOR ( 'NONE', #140017, 1000.000000000000227 ) ;
#113754=VERTEX_POINT ( 'NONE', #136847 ) ;
#113756=VERTEX_POINT ( 'NONE', #37559 ) ;
#113757=EDGE_CURVE ( 'NONE', #132084, #49722, #125266, .T. ) ;
#113758=CARTESIAN_POINT ( 'NONE',  ( 34.17183060077623225, -20.24070752338407786, 4.000000000000000000 ) ) ;
#113760=CARTESIAN_POINT ( 'NONE',  ( -0.7071067811865398012, 2.259292476615692546, 5.000000000000000000 ) ) ;
#113761=CARTESIAN_POINT ( 'NONE',  ( -1.499999999999987566, -6.839392718269127869, -8.480912228396080721 ) ) ;
#113762=CARTESIAN_POINT ( 'NONE',  ( 34.92499999999998295, 5.816654386410395894, 4.500000000000000888 ) ) ;
#113763=EDGE_CURVE ( 'NONE', #32610, #71084, #134751, .T. ) ;
#113765=DIRECTION ( 'NONE',  ( 0.7071067811865487940, 0.7071067811865463515, -0.000000000000000000 ) ) ;
#113768=CARTESIAN_POINT ( 'NONE',  ( 12.00548008471251293, 28.92564299267929684, 4.000000000000000000 ) ) ;
#113769=CARTESIAN_POINT ( 'NONE',  ( -16.01987774928538499, -17.24070752338410273, 20.23474786156465655 ) ) ;
#113770=VECTOR ( 'NONE', #109270, 1000.000000000000000 ) ;
#113771=FACE_OUTER_BOUND ( 'NONE', #30421, .T. ) ;
#113772=LINE ( 'NONE', #26059, #110276 ) ;
#113773=EDGE_LOOP ( 'NONE', ( #75076, #45798, #15314, #76740 ) ) ;
#113774=ORIENTED_EDGE ( 'NONE', *, *, #85383, .T. ) ;
#113777=AXIS2_PLACEMENT_3D ( 'NONE', #24330, #13423, #57704 ) ;
#113778=ORIENTED_EDGE ( 'NONE', *, *, #26492, .T. ) ;
#113781=CARTESIAN_POINT ( 'NONE',  ( -30.18398860626900060, 28.73617430169808173, 5.000000000000000000 ) ) ;
#113782=VECTOR ( 'NONE', #6519, 1000.000000000000227 ) ;
#113783=VECTOR ( 'NONE', #122474, 999.9999999999998863 ) ;
#113786=ORIENTED_EDGE ( 'NONE', *, *, #17750, .T. ) ;
#113787=CARTESIAN_POINT ( 'NONE',  ( 2.816011393730999401, 28.73617430169785436, 5.000000000000000000 ) ) ;
#113788=VECTOR ( 'NONE', #94278, 1000.000000000000227 ) ;
#113789=CARTESIAN_POINT ( 'NONE',  ( -34.92500000000001137, 2.464645009310397761, -2.487937186831662206 ) ) ;
#113790=CARTESIAN_POINT ( 'NONE',  ( -34.92500000000001137, 22.22500000000000142, 4.000000000000000000 ) ) ;
#113793=EDGE_CURVE ( 'NONE', #45578, #23228, #123862, .T. ) ;
#113794=PLANE ( 'NONE',  #142265 ) ;
#113795=VECTOR ( 'NONE', #100266, 1000.000000000000114 ) ;
#113797=CARTESIAN_POINT ( 'NONE',  ( -39.48921356237310221, -27.52281430457082934, 5.000000000000000000 ) ) ;
#113798=CARTESIAN_POINT ( 'NONE',  ( 26.99451991528749417, 28.92564299267956685, 4.000000000000000000 ) ) ;
#113799=DIRECTION ( 'NONE',  ( -0.000000000000000000, -0.3543493200069152693, 0.9351131265310292928 ) ) ;
#113800=DIRECTION ( 'NONE',  ( 0.6830127018922181881, 0.6830127018922202975, -0.2588190451025214056 ) ) ;
#113801=EDGE_CURVE ( 'NONE', #28238, #56422, #113664, .T. ) ;
#113803=EDGE_LOOP ( 'NONE', ( #29364, #57002, #42138, #90974 ) ) ;
#113806=VECTOR ( 'NONE', #36481, 1000.000000000000000 ) ;
#113807=DIRECTION ( 'NONE',  ( 0.6830127018922181881, 0.6830127018922202975, -0.2588190451025214056 ) ) ;
#113809=CARTESIAN_POINT ( 'NONE',  ( 8.277185695429338352, -21.72500000000000142, 5.000000000000000000 ) ) ;
#113811=VECTOR ( 'NONE', #60200, 1000.000000000000227 ) ;
#113815=VERTEX_POINT ( 'NONE', #136134 ) ;
#113816=VERTEX_POINT ( 'NONE', #81067 ) ;
#113817=DIRECTION ( 'NONE',  ( -0.3543493200069163240, 4.681814790819596721E-17, -0.9351131265310288487 ) ) ;
#113818=AXIS2_PLACEMENT_3D ( 'NONE', #72455, #63699, #107859 ) ;
#113819=ORIENTED_EDGE ( 'NONE', *, *, #109895, .T. ) ;
#113820=ORIENTED_EDGE ( 'NONE', *, *, #134517, .T. ) ;
#113821=VERTEX_POINT ( 'NONE', #19359 ) ;
#113822=CARTESIAN_POINT ( 'NONE',  ( -34.92500000000001137, 21.72500000000000142, 5.000000000000000000 ) ) ;
#113823=EDGE_CURVE ( 'NONE', #10224, #68931, #106303, .T. ) ;
#113824=VECTOR ( 'NONE', #116348, 1000.000000000000000 ) ;
#113825=VERTEX_POINT ( 'NONE', #16471 ) ;
#113826=VERTEX_POINT ( 'NONE', #8433 ) ;
#113828=ORIENTED_EDGE ( 'NONE', *, *, #47489, .T. ) ;
#113829=EDGE_LOOP ( 'NONE', ( #91431, #119183, #64255, #83662, #101949, #120327 ) ) ;
#113830=VECTOR ( 'NONE', #741, 1000.000000000000000 ) ;
#113831=VECTOR ( 'NONE', #98071, 1000.000000000000227 ) ;
#113832=CARTESIAN_POINT ( 'NONE',  ( 26.29289321881327623, -0.7407075233842718154, 5.000000000000000000 ) ) ;
#113833=CARTESIAN_POINT ( 'NONE',  ( 17.29289321881333663, 20.25929247661551713, 5.000000000000000000 ) ) ;
#113834=CARTESIAN_POINT ( 'NONE',  ( -51.48921356237309510, -27.52281430457091460, 5.000000000000000000 ) ) ;
#113835=ORIENTED_EDGE ( 'NONE', *, *, #71000, .T. ) ;
#113836=CARTESIAN_POINT ( 'NONE',  ( 0.000000000000000000, 0.000000000000000000, 5.000000000000000000 ) ) ;
#113837=AXIS2_PLACEMENT_3D ( 'NONE', #107794, #62186, #7025 ) ;
#113838=EDGE_CURVE ( 'NONE', #94040, #28957, #51996, .T. ) ;
#113839=DIRECTION ( 'NONE',  ( -0.7071067811865486830, -0.7071067811865464625, -0.000000000000000000 ) ) ;
#113840=FACE_OUTER_BOUND ( 'NONE', #31077, .T. ) ;
#113842=FACE_BOUND ( 'NONE', #44504, .T. ) ;
#113843=ORIENTED_EDGE ( 'NONE', *, *, #108113, .T. ) ;
#113846=FACE_OUTER_BOUND ( 'NONE', #42995, .T. ) ;
#113848=CARTESIAN_POINT ( 'NONE',  ( -48.18398860626899705, 28.73617430169820608, 5.000000000000000000 ) ) ;
#113850=VERTEX_POINT ( 'NONE', #63612 ) ;
#113851=VECTOR ( 'NONE', #38736, 1000.000000000000000 ) ;
#113852=ORIENTED_EDGE ( 'NONE', *, *, #56801, .F. ) ;
#113853=EDGE_CURVE ( 'NONE', #25222, #53667, #95478, .T. ) ;
#113856=DIRECTION ( 'NONE',  ( -0.7071067811865487940, 0.7071067811865463515, 0.000000000000000000 ) ) ;
#113857=EDGE_CURVE ( 'NONE', #26091, #89877, #52688, .T. ) ;
#113858=EDGE_CURVE ( 'NONE', #51446, #93029, #107772, .T. ) ;
#113860=CARTESIAN_POINT ( 'NONE',  ( -9.005480084712511157, 28.92564299267931816, 4.000000000000000000 ) ) ;
#113861=EDGE_LOOP ( 'NONE', ( #8093, #124256, #88282, #138201 ) ) ;
#113862=EDGE_CURVE ( 'NONE', #71344, #68553, #128825, .T. ) ;
#113863=CARTESIAN_POINT ( 'NONE',  ( -14.99999999999989342, -21.03360074219752462, 5.000000000000000000 ) ) ;
#113864=VECTOR ( 'NONE', #105841, 1000.000000000000000 ) ;
#113868=AXIS2_PLACEMENT_3D ( 'NONE', #127025, #84287, #114023 ) ;
#113869=DIRECTION ( 'NONE',  ( 0.7071067811865487940, 0.7071067811865463515, 0.000000000000000000 ) ) ;
#113870=LINE ( 'NONE', #122595, #69118 ) ;
#113871=FACE_OUTER_BOUND ( 'NONE', #41868, .T. ) ;
#113873=ORIENTED_EDGE ( 'NONE', *, *, #28768, .T. ) ;
#113874=ORIENTED_EDGE ( 'NONE', *, *, #2546, .T. ) ;
#113875=AXIS2_PLACEMENT_3D ( 'NONE', #28755, #138943, #96808 ) ;
#113876=ORIENTED_EDGE ( 'NONE', *, *, #140839, .T. ) ;
#113878=EDGE_LOOP ( 'NONE', ( #97679, #84915, #14130, #19823 ) ) ;
#113879=VECTOR ( 'NONE', #115735, 1000.000000000000000 ) ;
#113881=ORIENTED_EDGE ( 'NONE', *, *, #8101, .T. ) ;
#113882=ORIENTED_EDGE ( 'NONE', *, *, #79559, .T. ) ;
#113883=DIRECTION ( 'NONE',  ( 0.7071067811865487940, 0.7071067811865463515, 0.000000000000000000 ) ) ;
#113884=ADVANCED_FACE ( 'NONE', ( #51289 ), #5599, .F. ) ;
#113885=EDGE_CURVE ( 'NONE', #106778, #113634, #141120, .T. ) ;
#113886=DIRECTION ( 'NONE',  ( 0.7071067811865487940, 0.7071067811865463515, -0.000000000000000000 ) ) ;
#113887=ORIENTED_EDGE ( 'NONE', *, *, #24278, .F. ) ;
#113888=DIRECTION ( 'NONE',  ( 0.7071067811865486830, -0.7071067811865464625, -0.000000000000000000 ) ) ;
#113889=ORIENTED_EDGE ( 'NONE', *, *, #41838, .T. ) ;
#113890=EDGE_CURVE ( 'NONE', #16704, #106916, #85305, .T. ) ;
#113892=CARTESIAN_POINT ( 'NONE',  ( -0.1839886062690032631, 28.73617430169787568, 5.000000000000000000 ) ) ;
#113894=EDGE_LOOP ( 'NONE', ( #16838, #59001, #54725, #68564 ) ) ;
#113896=LINE ( 'NONE', #90743, #63855 ) ;
#113897=CARTESIAN_POINT ( 'NONE',  ( 57.48921356237308800, -27.52281430457095368, 5.000000000000000000 ) ) ;
#113898=CARTESIAN_POINT ( 'NONE',  ( -9.299744871391588674, -27.71228299555212971, 4.000000000000000000 ) ) ;
#113899=VERTEX_POINT ( 'NONE', #75199 ) ;
#113900=FILL_AREA_STYLE ('',( #69718 ) ) ;
#113902=CARTESIAN_POINT ( 'NONE',  ( 4.499999999999962697, 22.08746187583903975, 4.000000000000000000 ) ) ;
#113903=CARTESIAN_POINT ( 'NONE',  ( 21.18398860626899349, 28.73617430169802134, 5.000000000000000000 ) ) ;
#113904=LINE ( 'NONE', #71139, #38194 ) ;
#113905=CARTESIAN_POINT ( 'NONE',  ( 20.99999999999985079, -19.22509904557634641, 1.855685503482227494 ) ) ;
#113907=ORIENTED_EDGE ( 'NONE', *, *, #87878, .F. ) ;
#113908=VECTOR ( 'NONE', #21512, 999.9999999999998863 ) ;
#113909=CARTESIAN_POINT ( 'NONE',  ( 74.99451991528749772, 28.92564299267990435, 4.000000000000000000 ) ) ;
#113910=VECTOR ( 'NONE', #135935, 1000.000000000000227 ) ;
#113911=VECTOR ( 'NONE', #25265, 999.9999999999998863 ) ;
#113912=FACE_OUTER_BOUND ( 'NONE', #34895, .T. ) ;
#113913=LINE ( 'NONE', #127657, #39884 ) ;
#113914=EDGE_CURVE ( 'NONE', #56087, #25521, #41109, .T. ) ;
#113915=ORIENTED_EDGE ( 'NONE', *, *, #133066, .F. ) ;
#113916=LINE ( 'NONE', #127659, #2579 ) ;
#113917=VECTOR ( 'NONE', #104863, 1000.000000000000000 ) ;
#113918=CARTESIAN_POINT ( 'NONE',  ( -12.00548008471251293, 28.92564299267929684, 4.000000000000000000 ) ) ;
#113919=ORIENTED_EDGE ( 'NONE', *, *, #53288, .F. ) ;
#113920=CARTESIAN_POINT ( 'NONE',  ( -14.84387692260748182, -22.22499999999999787, 4.000000000000000000 ) ) ;
#113924=CARTESIAN_POINT ( 'NONE',  ( 0.000000000000000000, 0.000000000000000000, 5.000000000000000000 ) ) ;
#113925=ORIENTED_EDGE ( 'NONE', *, *, #78870, .F. ) ;
#113926=EDGE_CURVE ( 'NONE', #88472, #861, #73733, .T. ) ;
#113927=DIRECTION ( 'NONE',  ( -0.000000000000000000, 0.3543493200069153248, 0.9351131265310292928 ) ) ;
#113928=ORIENTED_EDGE ( 'NONE', *, *, #121229, .T. ) ;
#113930=LINE ( 'NONE', #135696, #104501 ) ;
#113931=EDGE_CURVE ( 'NONE', #108305, #88917, #106328, .T. ) ;
#113933=VECTOR ( 'NONE', #16621, 999.9999999999998863 ) ;
#113934=LINE ( 'NONE', #71172, #123457 ) ;
#113935=CARTESIAN_POINT ( 'NONE',  ( 31.49999999999978684, -11.94781430457070392, 5.000000000000000000 ) ) ;
#113936=VECTOR ( 'NONE', #81895, 1000.000000000000000 ) ;
#113937=CARTESIAN_POINT ( 'NONE',  ( 11.99451991528749417, 28.92564299267946382, 4.000000000000000000 ) ) ;
#113939=CARTESIAN_POINT ( 'NONE',  ( -12.70710678118645198, -18.74070752338409562, 5.000000000000000000 ) ) ;
#113940=ORIENTED_EDGE ( 'NONE', *, *, #50342, .F. ) ;
#113941=EDGE_LOOP ( 'NONE', ( #105235, #69857, #134199, #45126 ) ) ;
#113942=ORIENTED_EDGE ( 'NONE', *, *, #63758, .T. ) ;
#113945=EDGE_LOOP ( 'NONE', ( #6092, #107575, #80365, #9513 ) ) ;
#113947=ORIENTED_EDGE ( 'NONE', *, *, #38885, .F. ) ;
#113948=VECTOR ( 'NONE', #104996, 1000.000000000000000 ) ;
#113952=( BOUNDED_CURVE ( )  B_SPLINE_CURVE ( 3, ( #94673, #130919, #117839, #51923 ),
 .UNSPECIFIED., .F., .T. ) 
 B_SPLINE_CURVE_WITH_KNOTS ( ( 4, 4 ),
 ( 5.005968288816722733, 5.074607125596334534 ),
 .UNSPECIFIED. ) 
 CURVE ( )  GEOMETRIC_REPRESENTATION_ITEM ( )  RATIONAL_B_SPLINE_CURVE ( ( 1.000000000000000000, 0.9996074310407765395, 0.9996074310407765395, 1.000000000000000000 ) ) 
 REPRESENTATION_ITEM ( '' )  );
#113953=LINE ( 'NONE', #48011, #48531 ) ;
#113954=DIRECTION ( 'NONE',  ( 0.7071067811865487940, 0.7071067811865463515, -0.000000000000000000 ) ) ;
#113955=LINE ( 'NONE', #126265, #111360 ) ;
#113958=VERTEX_POINT ( 'NONE', #30227 ) ;
#113959=EDGE_CURVE ( 'NONE', #126961, #66021, #17216, .T. ) ;
#113960=CARTESIAN_POINT ( 'NONE',  ( -41.99451991528749062, 28.92564299267967343, 4.000000000000000000 ) ) ;
#113961=CARTESIAN_POINT ( 'NONE',  ( 11.99999999999991651, -0.8619312979531862373, -5.102805207349797811 ) ) ;
#113962=DIRECTION ( 'NONE',  ( 0.7071067811865487940, 0.7071067811865463515, 0.000000000000000000 ) ) ;
#113963=VECTOR ( 'NONE', #130545, 1000.000000000000000 ) ;
#113966=LINE ( 'NONE', #126273, #44678 ) ;
#113967=CARTESIAN_POINT ( 'NONE',  ( -31.49999999999977973, -2.173586137069170032, -4.605770156576181940 ) ) ;
#113969=CARTESIAN_POINT ( 'NONE',  ( 24.18398860626899705, 28.73617430169804265, 5.000000000000000000 ) ) ;
#113970=DIRECTION ( 'NONE',  ( -0.3543493200069162685, -0.000000000000000000, -0.9351131265310288487 ) ) ;
#113971=ORIENTED_EDGE ( 'NONE', *, *, #93603, .F. ) ;
#113972=ORIENTED_EDGE ( 'NONE', *, *, #125868, .T. ) ;
#113975=ORIENTED_EDGE ( 'NONE', *, *, #110429, .F. ) ;
#113976=DIRECTION ( 'NONE',  ( -0.7071067811865487940, 0.7071067811865463515, 0.000000000000000000 ) ) ;
#113977=CARTESIAN_POINT ( 'NONE',  ( -26.99999999999979750, 17.58746187583906462, 4.000000000000000000 ) ) ;
#113978=EDGE_LOOP ( 'NONE', ( #88762, #79638, #72168, #137829 ) ) ;
#113979=VECTOR ( 'NONE', #107973, 1000.000000000000000 ) ;
#113980=AXIS2_PLACEMENT_3D ( 'NONE', #67308, #80341, #111508 ) ;
#113981=PLANE ( 'NONE',  #131196 ) ;
#113982=CARTESIAN_POINT ( 'NONE',  ( -20.99999999999985079, -18.41253812416056945, 4.000000000000000000 ) ) ;
#113983=AXIS2_PLACEMENT_3D ( 'NONE', #15597, #138151, #91772 ) ;
#113984=CARTESIAN_POINT ( 'NONE',  ( -14.29298673570684919, -21.74070752338405299, 4.999753212805220670 ) ) ;
#113987=EDGE_CURVE ( 'NONE', #5793, #56807, #99038, .T. ) ;
#113989=EDGE_CURVE ( 'NONE', #14910, #33281, #100504, .T. ) ;
#113992=VECTOR ( 'NONE', #56794, 1000.000000000000000 ) ;
#113995=CARTESIAN_POINT ( 'NONE',  ( -54.18398860626899705, 28.73617430169825226, 5.000000000000000000 ) ) ;
#113998=ORIENTED_EDGE ( 'NONE', *, *, #127772, .F. ) ;
#113999=EDGE_CURVE ( 'NONE', #95318, #10073, #53412, .T. ) ;
#114000=ORIENTED_EDGE ( 'NONE', *, *, #123500, .F. ) ;
#114002=EDGE_CURVE ( 'NONE', #7775, #121162, #54173, .T. ) ;
#114003=DIRECTION ( 'NONE',  ( -0.7071067811865486830, 0.7071067811865464625, 0.000000000000000000 ) ) ;
#114004=DIRECTION ( 'NONE',  ( -0.000000000000000000, -0.3543493200069152693, 0.9351131265310292928 ) ) ;
#114006=DIRECTION ( 'NONE',  ( 0.7071067811865487940, 0.7071067811865463515, -0.000000000000000000 ) ) ;
#114007=CARTESIAN_POINT ( 'NONE',  ( 0.1839886062690032631, 28.73617430169787568, 5.000000000000000000 ) ) ;
#114008=EDGE_LOOP ( 'NONE', ( #82294, #119221, #61973, #114452 ) ) ;
#114010=DIRECTION ( 'NONE',  ( 0.6830127018922181881, 0.6830127018922202975, -0.2588190451025214056 ) ) ;
#114012=EDGE_CURVE ( 'NONE', #94430, #60173, #22889, .T. ) ;
#114013=VECTOR ( 'NONE', #43805, 1000.000000000000000 ) ;
#114016=ORIENTED_EDGE ( 'NONE', *, *, #27290, .T. ) ;
#114018=CARTESIAN_POINT ( 'NONE',  ( -34.42500000000001137, 0.000000000000000000, 4.500000000000000888 ) ) ;
#114019=AXIS2_PLACEMENT_3D ( 'NONE', #89046, #44103, #123092 ) ;
#114021=FACE_BOUND ( 'NONE', #84405, .T. ) ;
#114023=DIRECTION ( 'NONE',  ( -0.7071067811865486830, 0.7071067811865464625, 0.000000000000000000 ) ) ;
#114024=PLANE ( 'NONE',  #1634 ) ;
#114025=DIRECTION ( 'NONE',  ( 0.000000000000000000, 0.000000000000000000, -1.000000000000000000 ) ) ;
#114026=ORIENTED_EDGE ( 'NONE', *, *, #55361, .F. ) ;
#114028=VERTEX_POINT ( 'NONE', #86773 ) ;
#114029=EDGE_CURVE ( 'NONE', #46180, #124509, #65768, .T. ) ;
#114030=ORIENTED_EDGE ( 'NONE', *, *, #129132, .T. ) ;
#114032=VERTEX_POINT ( 'NONE', #22192 ) ;
#114033=LINE ( 'NONE', #45953, #48742 ) ;
#114034=ADVANCED_FACE ( 'NONE', ( #31672 ), #55576, .F. ) ;
#114036=VERTEX_POINT ( 'NONE', #75890 ) ;
#114039=EDGE_CURVE ( 'NONE', #43696, #4583, #24187, .T. ) ;
#114040=DIRECTION ( 'NONE',  ( 0.6830127018922181881, 0.6830127018922202975, -0.2588190451025214056 ) ) ;
#114042=DIRECTION ( 'NONE',  ( 1.000000000000000000, 0.000000000000000000, 0.000000000000000000 ) ) ;
#114043=LINE ( 'NONE', #74858, #6433 ) ;
#114044=CARTESIAN_POINT ( 'NONE',  ( -17.22995720542194675, 21.73644205237997440, 5.000000000000000888 ) ) ;
#114045=FACE_OUTER_BOUND ( 'NONE', #83715, .T. ) ;
#114046=LINE ( 'NONE', #14736, #41657 ) ;
#114047=ORIENTED_EDGE ( 'NONE', *, *, #101716, .T. ) ;
#114048=ORIENTED_EDGE ( 'NONE', *, *, #9758, .F. ) ;
#114049=CARTESIAN_POINT ( 'NONE',  ( 31.49999999999978684, 3.073033219394658122, -6.593910359670897670 ) ) ;
#114050=DIRECTION ( 'NONE',  ( 0.7071067811865486830, -0.7071067811865464625, -0.000000000000000000 ) ) ;
#114054=EDGE_CURVE ( 'NONE', #38978, #27213, #119357, .T. ) ;
#114055=ADVANCED_FACE ( 'NONE', ( #12038 ), #87481, .F. ) ;
#114058=ORIENTED_EDGE ( 'NONE', *, *, #12886, .T. ) ;
#114059=DIRECTION ( 'NONE',  ( -0.7071067811865487940, 0.7071067811865463515, 0.000000000000000000 ) ) ;
#114061=LINE ( 'NONE', #57571, #49337 ) ;
#114064=ORIENTED_EDGE ( 'NONE', *, *, #57741, .F. ) ;
#114065=CARTESIAN_POINT ( 'NONE',  ( -34.42500000000001137, -22.22500000000000142, 5.000000000000000000 ) ) ;
#114066=LINE ( 'NONE', #101762, #67463 ) ;
#114068=EDGE_CURVE ( 'NONE', #42161, #63574, #76627, .T. ) ;
#114070=CARTESIAN_POINT ( 'NONE',  ( -63.18398860626900415, 28.73617430169831621, 5.000000000000000000 ) ) ;
#114074=LINE ( 'NONE', #127084, #84364 ) ;
#114075=DIRECTION ( 'NONE',  ( -0.000000000000000000, 0.000000000000000000, 1.000000000000000000 ) ) ;
#114076=VECTOR ( 'NONE', #14597, 1000.000000000000227 ) ;
#114077=CARTESIAN_POINT ( 'NONE',  ( -3.343500094706353121, -22.22500000000000142, -6.967410892577142079 ) ) ;
#114078=VECTOR ( 'NONE', #40095, 1000.000000000000000 ) ;
#114082=LINE ( 'NONE', #103197, #44879 ) ;
#114083=DIRECTION ( 'NONE',  ( -0.6830127018922181881, 0.6830127018922202975, -0.2588190451025214056 ) ) ;
#114084=FACE_OUTER_BOUND ( 'NONE', #20782, .T. ) ;
#114085=VECTOR ( 'NONE', #94096, 999.9999999999998863 ) ;
#114086=ADVANCED_FACE ( 'NONE', ( #10599 ), #143274, .F. ) ;
#114088=ORIENTED_EDGE ( 'NONE', *, *, #87402, .F. ) ;
#114090=LINE ( 'NONE', #3848, #67041 ) ;
#114091=LINE ( 'NONE', #114773, #53924 ) ;
#114093=DIRECTION ( 'NONE',  ( 0.3543493200069163240, 0.000000000000000000, -0.9351131265310288487 ) ) ;
#114094=DIRECTION ( 'NONE',  ( -0.3543493200069162685, -0.000000000000000000, -0.9351131265310288487 ) ) ;
#114096=EDGE_CURVE ( 'NONE', #99824, #13806, #33140, .T. ) ;
#114097=EDGE_LOOP ( 'NONE', ( #113142, #64658, #95883, #112151 ) ) ;
#114099=LINE ( 'NONE', #34400, #27128 ) ;
#114100=DIRECTION ( 'NONE',  ( 1.000000000000000000, 0.000000000000000000, 0.000000000000000000 ) ) ;
#114104=VECTOR ( 'NONE', #98932, 1000.000000000000000 ) ;
#114105=LINE ( 'NONE', #116951, #41537 ) ;
#114106=LINE ( 'NONE', #1726, #136256 ) ;
#114107=DIRECTION ( 'NONE',  ( 0.7071067811865486830, -0.7071067811865464625, -0.000000000000000000 ) ) ;
#114108=VERTEX_POINT ( 'NONE', #101916 ) ;
#114109=LINE ( 'NONE', #103221, #11763 ) ;
#114110=DIRECTION ( 'NONE',  ( -0.7071067811865486830, -0.7071067811865464625, 0.000000000000000000 ) ) ;
#114111=CARTESIAN_POINT ( 'NONE',  ( -48.18398860626899705, 28.73617430169820608, 5.000000000000000000 ) ) ;
#114113=AXIS2_PLACEMENT_3D ( 'NONE', #83964, #62191, #116555 ) ;
#114115=CARTESIAN_POINT ( 'NONE',  ( -34.92500000000001137, 5.816654386410375466, 4.500000000000000888 ) ) ;
#114117=ORIENTED_EDGE ( 'NONE', *, *, #96503, .F. ) ;
#114119=ORIENTED_EDGE ( 'NONE', *, *, #78242, .F. ) ;
#114120=CARTESIAN_POINT ( 'NONE',  ( 25.49999999999982592, 3.431123077392145948, 4.000000000000000000 ) ) ;
#114122=PLANE ( 'NONE',  #88232 ) ;
#114123=CARTESIAN_POINT ( 'NONE',  ( 0.000000000000000000, 0.000000000000000000, 5.000000000000000000 ) ) ;
#114124=CARTESIAN_POINT ( 'NONE',  ( -66.18398860626901126, 28.73617430169833753, 5.000000000000000000 ) ) ;
#114125=DIRECTION ( 'NONE',  ( 0.000000000000000000, -1.000000000000000000, 0.000000000000000000 ) ) ;
#114126=ORIENTED_EDGE ( 'NONE', *, *, #594, .F. ) ;
#114127=ORIENTED_EDGE ( 'NONE', *, *, #70637, .T. ) ;
#114128=CARTESIAN_POINT ( 'NONE',  ( -75.29974487139158157, -27.71228299555258445, 4.000000000000000000 ) ) ;
#114129=LINE ( 'NONE', #92355, #5197 ) ;
#114132=( BOUNDED_CURVE ( )  B_SPLINE_CURVE ( 3, ( #103856, #136506, #124926, #82870 ),
 .UNSPECIFIED., .F., .T. ) 
 B_SPLINE_CURVE_WITH_KNOTS ( ( 4, 4 ),
 ( 0.06988172079111230894, 0.1872541115065302075 ),
 .UNSPECIFIED. ) 
 CURVE ( )  GEOMETRIC_REPRESENTATION_ITEM ( )  RATIONAL_B_SPLINE_CURVE ( ( 1.000000000000000000, 0.9988523062762910687, 0.9988523062762910687, 1.000000000000000000 ) ) 
 REPRESENTATION_ITEM ( '' )  );
#114133=CARTESIAN_POINT ( 'NONE',  ( 21.72281430457044493, -21.72500000000000142, 5.000000000000000000 ) ) ;
#114138=CARTESIAN_POINT ( 'NONE',  ( 8.207106781186487510, -20.24070752338407431, 5.000000000000000000 ) ) ;
#114139=LINE ( 'NONE', #14824, #106442 ) ;
#114140=CARTESIAN_POINT ( 'NONE',  ( 4.499999999999976019, 0.4497235411627491519, -5.599840258123530035 ) ) ;
#114141=VECTOR ( 'NONE', #81417, 1000.000000000000000 ) ;
#114142=EDGE_CURVE ( 'NONE', #140579, #32809, #80891, .T. ) ;
#114143=VECTOR ( 'NONE', #142339, 1000.000000000000000 ) ;
#114144=ORIENTED_EDGE ( 'NONE', *, *, #75665, .T. ) ;
#114145=DIRECTION ( 'NONE',  ( -0.6830127018922180770, -0.6830127018922204085, -0.2588190451025213501 ) ) ;
#114148=DIRECTION ( 'NONE',  ( 1.000000000000000000, 0.000000000000000000, 0.000000000000000000 ) ) ;
#114150=VERTEX_POINT ( 'NONE', #48981 ) ;
#114151=VECTOR ( 'NONE', #81591, 999.9999999999998863 ) ;
#114152=CARTESIAN_POINT ( 'NONE',  ( 27.81349135397621453, -15.74070752338412760, 8.904080028138874781 ) ) ;
#114153=DIRECTION ( 'NONE',  ( -0.7071067811865486830, 0.7071067811865464625, 0.000000000000000000 ) ) ;
#114155=EDGE_CURVE ( 'NONE', #28590, #126135, #4682, .T. ) ;
#114156=CARTESIAN_POINT ( 'NONE',  ( 72.48921356237309510, -27.52281430457106026, 5.000000000000000000 ) ) ;
#114157=DIRECTION ( 'NONE',  ( -0.000000000000000000, -0.3543493200069152693, 0.9351131265310292928 ) ) ;
#114159=EDGE_CURVE ( 'NONE', #133751, #54071, #53847, .T. ) ;
#114160=PLANE ( 'NONE',  #115539 ) ;
#114161=CARTESIAN_POINT ( 'NONE',  ( -45.18398860626900415, 28.73617430169818832, 5.000000000000000000 ) ) ;
#114162=AXIS2_PLACEMENT_3D ( 'NONE', #134694, #80313, #23769 ) ;
#114163=CARTESIAN_POINT ( 'NONE',  ( 42.48921356237308800, -27.52281430457085065, 5.000000000000000000 ) ) ;
#114164=CARTESIAN_POINT ( 'NONE',  ( 42.18398860626899705, 28.73617430169816700, 5.000000000000000000 ) ) ;
#114165=ORIENTED_EDGE ( 'NONE', *, *, #23148, .F. ) ;
#114166=ORIENTED_EDGE ( 'NONE', *, *, #87740, .T. ) ;
#114167=EDGE_CURVE ( 'NONE', #57842, #129322, #25052, .T. ) ;
#114169=LINE ( 'NONE', #14853, #90384 ) ;
#114171=CARTESIAN_POINT ( 'NONE',  ( -14.99451991528749595, 28.92564299267948513, 4.000000000000000000 ) ) ;
#114172=CARTESIAN_POINT ( 'NONE',  ( -5.994519915287488843, 28.92564299267942118, 4.000000000000000000 ) ) ;
#114173=ORIENTED_EDGE ( 'NONE', *, *, #85351, .T. ) ;
#114174=VERTEX_POINT ( 'NONE', #15572 ) ;
#114176=LINE ( 'NONE', #135252, #33065 ) ;
#114177=PLANE ( 'NONE',  #102319 ) ;
#114178=ADVANCED_FACE ( 'NONE', ( #59853 ), #104020, .F. ) ;
#114179=VECTOR ( 'NONE', #86959, 1000.000000000000227 ) ;
#114180=ORIENTED_EDGE ( 'NONE', *, *, #265, .F. ) ;
#114181=ORIENTED_EDGE ( 'NONE', *, *, #39044, .F. ) ;
#114182=LINE ( 'NONE', #59142, #135947 ) ;
#114183=FACE_OUTER_BOUND ( 'NONE', #143033, .T. ) ;
#114184=VECTOR ( 'NONE', #103882, 1000.000000000000227 ) ;
#114186=ADVANCED_FACE ( 'NONE', ( #91745 ), #113487, .F. ) ;
#114187=ORIENTED_EDGE ( 'NONE', *, *, #80662, .T. ) ;
#114188=FACE_BOUND ( 'NONE', #127185, .T. ) ;
#114189=DIRECTION ( 'NONE',  ( -0.000000000000000000, 0.000000000000000000, 1.000000000000000000 ) ) ;
#114190=CARTESIAN_POINT ( 'NONE',  ( -11.81601139373100651, 28.73617430169779041, 5.000000000000000000 ) ) ;
#114191=CARTESIAN_POINT ( 'NONE',  ( 68.99451991528748351, 28.92564299267986172, 4.000000000000000000 ) ) ;
#114193=DIRECTION ( 'NONE',  ( 1.000000000000000000, 0.000000000000000000, 0.000000000000000000 ) ) ;
#114195=ORIENTED_EDGE ( 'NONE', *, *, #121931, .T. ) ;
#114196=VECTOR ( 'NONE', #20308, 1000.000000000000000 ) ;
#114197=VERTEX_POINT ( 'NONE', #112099 ) ;
#114199=VERTEX_POINT ( 'NONE', #80197 ) ;
#114200=DIRECTION ( 'NONE',  ( 0.6830127018922181881, 0.6830127018922202975, -0.2588190451025214056 ) ) ;
#114201=ADVANCED_FACE ( 'NONE', ( #102650 ), #12747, .F. ) ;
#114202=DIRECTION ( 'NONE',  ( 0.7071067811865487940, 0.7071067811865463515, 0.000000000000000000 ) ) ;
#114203=VECTOR ( 'NONE', #88776, 999.9999999999998863 ) ;
#114204=LINE ( 'NONE', #12738, #6121 ) ;
#114205=EDGE_CURVE ( 'NONE', #125931, #97996, #101195, .T. ) ;
#114206=EDGE_CURVE ( 'NONE', #121707, #120720, #35269, .T. ) ;
#114207=CARTESIAN_POINT ( 'NONE',  ( -56.99451991528749062, 28.92564299267978001, 4.000000000000000000 ) ) ;
#114208=VERTEX_POINT ( 'NONE', #47584 ) ;
#114209=DIRECTION ( 'NONE',  ( 0.7071067811865487940, 0.7071067811865463515, 0.000000000000000000 ) ) ;
#114210=FACE_OUTER_BOUND ( 'NONE', #107548, .T. ) ;
#114211=CIRCLE ( 'NONE', #81867, 5.968999999999998529 ) ;
#114213=LINE ( 'NONE', #46885, #59649 ) ;
#114214=PLANE ( 'NONE',  #142311 ) ;
#114215=LINE ( 'NONE', #14895, #134185 ) ;
#114217=ORIENTED_EDGE ( 'NONE', *, *, #13989, .F. ) ;
#114218=EDGE_CURVE ( 'NONE', #95318, #22921, #68600, .T. ) ;
#114219=CARTESIAN_POINT ( 'NONE',  ( 11.30673006690394189, -3.740707523384244837, 12.88036043432864908 ) ) ;
#114220=DIRECTION ( 'NONE',  ( 0.7071067811865487940, 0.7071067811865463515, 0.000000000000000000 ) ) ;
#114222=VERTEX_POINT ( 'NONE', #70052 ) ;
#114224=EDGE_CURVE ( 'NONE', #113754, #130071, #114215, .T. ) ;
#114225=ADVANCED_FACE ( 'NONE', ( #103319 ), #48248, .F. ) ;
#114226=ORIENTED_EDGE ( 'NONE', *, *, #140245, .T. ) ;
#114228=VERTEX_POINT ( 'NONE', #71442 ) ;
#114229=VECTOR ( 'NONE', #105453, 999.9999999999998863 ) ;
#114232=AXIS2_PLACEMENT_3D ( 'NONE', #71738, #59449, #137706 ) ;
#114235=ORIENTED_EDGE ( 'NONE', *, *, #17898, .T. ) ;
#114236=LINE ( 'NONE', #35288, #78054 ) ;
#114238=DIRECTION ( 'NONE',  ( 0.7071067811865487940, 0.7071067811865463515, 0.000000000000000000 ) ) ;
#114239=EDGE_CURVE ( 'NONE', #101225, #21579, #95315, .T. ) ;
#114241=ORIENTED_EDGE ( 'NONE', *, *, #38903, .F. ) ;
#114242=VERTEX_POINT ( 'NONE', #38808 ) ;
#114243=LINE ( 'NONE', #105490, #12137 ) ;
#114244=CARTESIAN_POINT ( 'NONE',  ( -22.49999999999984368, -17.91344420646044711, 1.358650452708411782 ) ) ;
#114245=DIRECTION ( 'NONE',  ( -0.6830127018922180770, -0.6830127018922204085, -0.2588190451025213501 ) ) ;
#114246=( BOUNDED_CURVE ( )  B_SPLINE_CURVE ( 3, ( #76392, #21286, #109715, #10386 ),
 .UNSPECIFIED., .F., .T. ) 
 B_SPLINE_CURVE_WITH_KNOTS ( ( 4, 4 ),
 ( 1.901594255663605182, 1.933014472006535422 ),
 .UNSPECIFIED. ) 
 CURVE ( )  GEOMETRIC_REPRESENTATION_ITEM ( )  RATIONAL_B_SPLINE_CURVE ( ( 1.000000000000000000, 0.9999177325257868620, 0.9999177325257868620, 1.000000000000000000 ) ) 
 REPRESENTATION_ITEM ( '' )  );
#114247=VERTEX_POINT ( 'NONE', #96707 ) ;
#114248=DIRECTION ( 'NONE',  ( -0.6830127018922181881, 0.6830127018922202975, -0.2588190451025214056 ) ) ;
#114249=VERTEX_POINT ( 'NONE', #117058 ) ;
#114250=VERTEX_POINT ( 'NONE', #139579 ) ;
#114252=ORIENTED_EDGE ( 'NONE', *, *, #6492, .F. ) ;
#114253=CARTESIAN_POINT ( 'NONE',  ( -38.99451991528749062, 28.92564299267965211, 4.000000000000000000 ) ) ;
#114254=CARTESIAN_POINT ( 'NONE',  ( -21.79289321881330466, 15.75929247661555976, 5.000000000000000000 ) ) ;
#114255=LINE ( 'NONE', #136713, #23896 ) ;
#114256=DIRECTION ( 'NONE',  ( -0.7071067811865486830, -0.7071067811865464625, 0.000000000000000000 ) ) ;
#114257=CARTESIAN_POINT ( 'NONE',  ( -24.18398860626899705, 28.73617430169804265, 5.000000000000000000 ) ) ;
#114259=ORIENTED_EDGE ( 'NONE', *, *, #69358, .F. ) ;
#114260=EDGE_CURVE ( 'NONE', #72669, #57481, #40263, .T. ) ;
#114261=ADVANCED_FACE ( 'NONE', ( #8275 ), #7577, .F. ) ;
#114262=EDGE_CURVE ( 'NONE', #50077, #60759, #5430, .T. ) ;
#114264=CARTESIAN_POINT ( 'NONE',  ( -18.53421140649331633, 9.121673282332597665, 4.000000000000000000 ) ) ;
#114266=CARTESIAN_POINT ( 'NONE',  ( 48.18398860626899705, 28.73617430169820608, 5.000000000000000000 ) ) ;
#114267=LINE ( 'NONE', #126553, #104557 ) ;
#114268=EDGE_LOOP ( 'NONE', ( #117137, #95437, #91650, #94063 ) ) ;
#114269=VERTEX_POINT ( 'NONE', #84474 ) ;
#114270=ORIENTED_EDGE ( 'NONE', *, *, #143065, .T. ) ;
#114271=DIRECTION ( 'NONE',  ( -0.7071067811865487940, 0.7071067811865463515, -0.000000000000000000 ) ) ;
#114272=CARTESIAN_POINT ( 'NONE',  ( 34.42499999999998295, 0.000000000000000000, 4.500000000000000888 ) ) ;
#114274=CARTESIAN_POINT ( 'NONE',  ( -6.489213562373093325, -27.52281430457059841, 5.000000000000000000 ) ) ;
#114275=CARTESIAN_POINT ( 'NONE',  ( -2.999999999999980016, 1.931123077392165488, 4.000000000000000000 ) ) ;
#114276=ADVANCED_FACE ( 'NONE', ( #51121 ), #106899, .F. ) ;
#114277=CARTESIAN_POINT ( 'NONE',  ( -5.999999999999963585, -2.904428200921325143, -6.989807076074931125 ) ) ;
#114278=DIRECTION ( 'NONE',  ( 0.7071067811865486830, -0.7071067811865464625, -0.000000000000000000 ) ) ;
#114280=DIRECTION ( 'NONE',  ( -0.000000000000000000, -0.3543493200069152693, 0.9351131265310292928 ) ) ;
#114281=DIRECTION ( 'NONE',  ( -0.6830127018922181881, 0.6830127018922202975, -0.2588190451025214056 ) ) ;
#114282=FACE_OUTER_BOUND ( 'NONE', #68628, .T. ) ;
#114283=DIRECTION ( 'NONE',  ( 1.000000000000000000, 0.000000000000000000, 0.000000000000000000 ) ) ;
#114284=CARTESIAN_POINT ( 'NONE',  ( 60.18398860626900415, 28.73617430169829490, 5.000000000000000000 ) ) ;
#114285=EDGE_LOOP ( 'NONE', ( #43044, #85724, #110349, #139920 ) ) ;
#114286=ORIENTED_EDGE ( 'NONE', *, *, #122197, .F. ) ;
#114287=CARTESIAN_POINT ( 'NONE',  ( -17.20710678118642889, 9.759292476615625489, 5.000000000000000000 ) ) ;
#114288=DIRECTION ( 'NONE',  ( -0.000000000000000000, -0.000000000000000000, 1.000000000000000000 ) ) ;
#114289=ORIENTED_EDGE ( 'NONE', *, *, #105418, .F. ) ;
#114290=PLANE ( 'NONE',  #23186 ) ;
#114293=ORIENTED_EDGE ( 'NONE', *, *, #10541, .F. ) ;
#114294=LINE ( 'NONE', #124461, #108594 ) ;
#114295=VERTEX_POINT ( 'NONE', #40947 ) ;
#114296=FACE_OUTER_BOUND ( 'NONE', #62443, .T. ) ;
#114297=ORIENTED_EDGE ( 'NONE', *, *, #19660, .F. ) ;
#114299=CARTESIAN_POINT ( 'NONE',  ( 5.292986735706907808, -21.74070752338406365, 4.999753212805221558 ) ) ;
#114301=CARTESIAN_POINT ( 'NONE',  ( -5.994519915287488843, 28.92564299267942118, 4.000000000000000000 ) ) ;
#114302=AXIS2_PLACEMENT_3D ( 'NONE', #44996, #89170, #137681 ) ;
#114303=LINE ( 'NONE', #70141, #46292 ) ;
#114304=VERTEX_POINT ( 'NONE', #115593 ) ;
#114305=CARTESIAN_POINT ( 'NONE',  ( -34.92500000000001137, -9.908632306349543839, -7.176634499130168265 ) ) ;
#114306=FACE_OUTER_BOUND ( 'NONE', #124991, .T. ) ;
#114307=FACE_OUTER_BOUND ( 'NONE', #33338, .T. ) ;
#114310=CARTESIAN_POINT ( 'NONE',  ( 24.48921356237309510, -27.52281430457072631, 5.000000000000000000 ) ) ;
#114312=ORIENTED_EDGE ( 'NONE', *, *, #109382, .F. ) ;
#114314=DIRECTION ( 'NONE',  ( -0.6830127018922181881, 0.6830127018922202975, -0.2588190451025214056 ) ) ;
#114315=ORIENTED_EDGE ( 'NONE', *, *, #1573, .F. ) ;
#114317=PLANE ( 'NONE',  #87157 ) ;
#114319=CARTESIAN_POINT ( 'NONE',  ( 34.45011844616453800, 19.51628081163730499, 5.000000000000001776 ) ) ;
#114320=CARTESIAN_POINT ( 'NONE',  ( -31.49999999999976552, 4.087461875839202285, 4.000000000000000000 ) ) ;
#114321=ORIENTED_EDGE ( 'NONE', *, *, #28317, .F. ) ;
#114322=DIRECTION ( 'NONE',  ( -0.7071067811865486830, -0.7071067811865464625, 0.000000000000000000 ) ) ;
#114323=VECTOR ( 'NONE', #132132, 1000.000000000000000 ) ;
#114324=ADVANCED_FACE ( 'NONE', ( #138843 ), #85149, .F. ) ;
#114326=ORIENTED_EDGE ( 'NONE', *, *, #123562, .T. ) ;
#114327=DIRECTION ( 'NONE',  ( -0.7071067811865486830, -0.7071067811865464625, 0.000000000000000000 ) ) ;
#114328=ADVANCED_FACE ( 'NONE', ( #73580 ), #29337, .F. ) ;
#114330=CARTESIAN_POINT ( 'NONE',  ( 5.994519915287488843, 28.92564299267942118, 4.000000000000000000 ) ) ;
#114331=EDGE_LOOP ( 'NONE', ( #141477, #47825, #19452, #21674 ) ) ;
#114332=LINE ( 'NONE', #15006, #8936 ) ;
#114333=CARTESIAN_POINT ( 'NONE',  ( 12.48921356237309155, -27.52281430457064104, 5.000000000000000000 ) ) ;
#114334=CARTESIAN_POINT ( 'NONE',  ( -25.49999999999981526, -5.947814304570765209, 5.000000000000000000 ) ) ;
#114336=VECTOR ( 'NONE', #127604, 1000.000000000000000 ) ;
#114338=ADVANCED_FACE ( 'NONE', ( #138120 ), #127219, .F. ) ;
#114341=VERTEX_POINT ( 'NONE', #72911 ) ;
#114343=AXIS2_PLACEMENT_3D ( 'NONE', #99231, #42770, #22384 ) ;
#114344=EDGE_LOOP ( 'NONE', ( #14940, #139396, #125101, #8991 ) ) ;
#114347=CARTESIAN_POINT ( 'NONE',  ( -29.67183060077626422, 14.25929247661557397, 4.000000000000000000 ) ) ;
#114349=LINE ( 'NONE', #15019, #142997 ) ;
#114350=CARTESIAN_POINT ( 'NONE',  ( 48.48921356237309510, -27.52281430457089328, 5.000000000000000000 ) ) ;
#114351=EDGE_LOOP ( 'NONE', ( #18509, #12862, #84693, #64593 ) ) ;
#114352=CARTESIAN_POINT ( 'NONE',  ( 14.19331503651554272, 6.646281381260698673, 4.665372575888455664 ) ) ;
#114353=CARTESIAN_POINT ( 'NONE',  ( -42.48921356237308800, -27.52281430457085065, 5.000000000000000000 ) ) ;
#114356=ORIENTED_EDGE ( 'NONE', *, *, #11523, .T. ) ;
#114357=DIRECTION ( 'NONE',  ( -0.6830127018922181881, 0.6830127018922202975, -0.2588190451025214056 ) ) ;
#114359=VECTOR ( 'NONE', #8147, 1000.000000000000000 ) ;
#114360=DIRECTION ( 'NONE',  ( -0.7071067811865486830, -0.7071067811865464625, 0.000000000000000000 ) ) ;
#114361=ADVANCED_FACE ( 'NONE', ( #131525 ), #143109, .F. ) ;
#114362=ORIENTED_EDGE ( 'NONE', *, *, #72000, .F. ) ;
#114363=ORIENTED_EDGE ( 'NONE', *, *, #70204, .T. ) ;
#114364=LINE ( 'NONE', #63419, #16808 ) ;
#114365=DIRECTION ( 'NONE',  ( -0.7071067811865486830, -0.7071067811865464625, 0.000000000000000000 ) ) ;
#114367=ADVANCED_FACE ( 'NONE', ( #65594 ), #22716, .F. ) ;
#114369=LINE ( 'NONE', #15040, #55775 ) ;
#114370=FACE_OUTER_BOUND ( 'NONE', #78931, .T. ) ;
#114371=CIRCLE ( 'NONE', #51890, 5.968999999999998529 ) ;
#114372=ORIENTED_EDGE ( 'NONE', *, *, #59991, .T. ) ;
#114373=EDGE_LOOP ( 'NONE', ( #115999, #60627, #31699, #74662 ) ) ;
#114374=LINE ( 'NONE', #13611, #138334 ) ;
#114375=ORIENTED_EDGE ( 'NONE', *, *, #40410, .T. ) ;
#114376=ADVANCED_FACE ( 'NONE', ( #88018 ), #85867, .F. ) ;
#114377=VECTOR ( 'NONE', #20048, 1000.000000000000000 ) ;
#114378=EDGE_CURVE ( 'NONE', #101569, #108829, #41647, .T. ) ;
#114379=DIRECTION ( 'NONE',  ( -0.7071067811865486830, -0.7071067811865464625, 0.000000000000000000 ) ) ;
#114380=ORIENTED_EDGE ( 'NONE', *, *, #63346, .F. ) ;
#114381=DIRECTION ( 'NONE',  ( -0.7071067811865486830, -0.7071067811865464625, 0.000000000000000000 ) ) ;
#114382=LINE ( 'NONE', #37557, #121206 ) ;
#114383=EDGE_CURVE ( 'NONE', #54251, #30424, #43802, .T. ) ;
#114384=FACE_OUTER_BOUND ( 'NONE', #69910, .T. ) ;
#114385=LINE ( 'NONE', #112263, #42119 ) ;
#114386=ORIENTED_EDGE ( 'NONE', *, *, #12751, .F. ) ;
#114387=ADVANCED_FACE ( 'NONE', ( #53992 ), #142415, .F. ) ;
#114388=PLANE ( 'NONE',  #56508 ) ;
#114389=CARTESIAN_POINT ( 'NONE',  ( -0.4892135623730947680, -27.52281430457055578, 5.000000000000000000 ) ) ;
#114391=CARTESIAN_POINT ( 'NONE',  ( -32.29298673570672662, -21.74070752338405299, 4.999753212805210012 ) ) ;
#114392=ORIENTED_EDGE ( 'NONE', *, *, #27781, .T. ) ;
#114394=CARTESIAN_POINT ( 'NONE',  ( -33.32816939922329880, 5.259292476615662792, 4.000000000000000000 ) ) ;
#114395=ORIENTED_EDGE ( 'NONE', *, *, #95104, .F. ) ;
#114398=AXIS2_PLACEMENT_3D ( 'NONE', #83032, #48985, #61326 ) ;
#114399=ORIENTED_EDGE ( 'NONE', *, *, #121097, .T. ) ;
#114400=CARTESIAN_POINT ( 'NONE',  ( 22.21321903303345024, 12.75929247661558641, 10.29404684609040643 ) ) ;
#114401=VECTOR ( 'NONE', #35002, 1000.000000000000227 ) ;
#114404=FACE_OUTER_BOUND ( 'NONE', #57732, .T. ) ;
#114406=CARTESIAN_POINT ( 'NONE',  ( -4.499999999999966249, -17.56887692260763245, 4.000000000000000000 ) ) ;
#114407=DIRECTION ( 'NONE',  ( 0.7071067811865487940, 0.7071067811865463515, 0.000000000000000000 ) ) ;
#114408=CARTESIAN_POINT ( 'NONE',  ( 5.700255128608413102, -27.71228299555201957, 4.000000000000000000 ) ) ;
#114409=ADVANCED_FACE ( 'NONE', ( #111168 ), #141696, .F. ) ;
#114410=LINE ( 'NONE', #24545, #102546 ) ;
#114413=EDGE_LOOP ( 'NONE', ( #81381, #123728, #127453, #67701 ) ) ;
#114415=AXIS2_PLACEMENT_3D ( 'NONE', #8491, #18675, #139800 ) ;
#114416=DIRECTION ( 'NONE',  ( 0.7071067811865486830, -0.7071067811865464625, -0.000000000000000000 ) ) ;
#114418=ORIENTED_EDGE ( 'NONE', *, *, #132398, .T. ) ;
#114419=EDGE_LOOP ( 'NONE', ( #44088, #135758, #107901, #61873 ) ) ;
#114420=CARTESIAN_POINT ( 'NONE',  ( 2.125146193092330105, -14.24070752338413470, 9.401115078912654965 ) ) ;
#114421=VERTEX_POINT ( 'NONE', #42398 ) ;
#114422=CARTESIAN_POINT ( 'NONE',  ( 54.48921356237310221, -27.52281430457093236, 5.000000000000000000 ) ) ;
#114423=DIRECTION ( 'NONE',  ( -0.000000000000000000, 0.3543493200069153248, 0.9351131265310292928 ) ) ;
#114424=COLOUR_RGB ( '', 0.31764706, 0.68627451, 0.89019608) ;
#114425=CARTESIAN_POINT ( 'NONE',  ( 34.42499999999998295, 5.977185695429338530, 5.000000000000000000 ) ) ;
#114426=FACE_OUTER_BOUND ( 'NONE', #130828, .T. ) ;
#114427=VERTEX_POINT ( 'NONE', #21336 ) ;
#114429=CARTESIAN_POINT ( 'NONE',  ( -27.32816939922333432, 8.259292476615641476, 4.000000000000000000 ) ) ;
#114430=VECTOR ( 'NONE', #52013, 1000.000000000000000 ) ;
#114431=EDGE_CURVE ( 'NONE', #107568, #49762, #132270, .T. ) ;
#114436=ORIENTED_EDGE ( 'NONE', *, *, #95997, .T. ) ;
#114437=ORIENTED_EDGE ( 'NONE', *, *, #109264, .F. ) ;
#114438=CARTESIAN_POINT ( 'NONE',  ( -22.49999999999984723, 18.05218569542898877, 5.000000000000000000 ) ) ;
#114439=DIRECTION ( 'NONE',  ( 0.3543493200069162685, -0.000000000000000000, -0.9351131265310288487 ) ) ;
#114440=LINE ( 'NONE', #102164, #142300 ) ;
#114442=ORIENTED_EDGE ( 'NONE', *, *, #25541, .T. ) ;
#114443=CARTESIAN_POINT ( 'NONE',  ( -9.183988606268997046, 28.73617430169793607, 5.000000000000000000 ) ) ;
#114444=DIRECTION ( 'NONE',  ( -0.000000000000000000, -0.3543493200069152693, 0.9351131265310292928 ) ) ;
#114445=AXIS2_PLACEMENT_3D ( 'NONE', #1670, #122047, #25595 ) ;
#114446=DIRECTION ( 'NONE',  ( -0.7071067811865487940, 0.7071067811865463515, 0.000000000000000000 ) ) ;
#114447=CARTESIAN_POINT ( 'NONE',  ( 0.000000000000000000, 0.000000000000000000, 5.000000000000000000 ) ) ;
#114448=ORIENTED_EDGE ( 'NONE', *, *, #30848, .T. ) ;
#114452=ORIENTED_EDGE ( 'NONE', *, *, #120268, .F. ) ;
#114453=ORIENTED_EDGE ( 'NONE', *, *, #118465, .F. ) ;
#114454=FACE_OUTER_BOUND ( 'NONE', #120089, .T. ) ;
#114456=VERTEX_POINT ( 'NONE', #86608 ) ;
#114458=CARTESIAN_POINT ( 'NONE',  ( 11.70025512860841133, -27.71228299555198049, 4.000000000000000000 ) ) ;
#114459=CARTESIAN_POINT ( 'NONE',  ( -3.183988606268992161, 28.73617430169789699, 5.000000000000000000 ) ) ;
#114461=DIRECTION ( 'NONE',  ( 0.7071067811865487940, 0.7071067811865463515, 0.000000000000000000 ) ) ;
#114463=FACE_OUTER_BOUND ( 'NONE', #88515, .T. ) ;
#114464=LINE ( 'NONE', #37657, #7789 ) ;
#114465=CARTESIAN_POINT ( 'NONE',  ( -48.29974487139158867, -27.71228299555239971, 4.000000000000000000 ) ) ;
#114467=LINE ( 'NONE', #112353, #104641 ) ;
#114468=CARTESIAN_POINT ( 'NONE',  ( 22.49999999999984013, -1.592773361805351673, -6.492772025301281502 ) ) ;
#114469=FACE_OUTER_BOUND ( 'NONE', #64264, .T. ) ;
#114470=DIRECTION ( 'NONE',  ( -0.000000000000000000, -0.3543493200069152693, 0.9351131265310292928 ) ) ;
#114471=ORIENTED_EDGE ( 'NONE', *, *, #123718, .F. ) ;
#114472=VECTOR ( 'NONE', #85495, 1000.000000000000000 ) ;
#114473=EDGE_LOOP ( 'NONE', ( #74651, #68593, #41664, #46214 ) ) ;
#114475=ORIENTED_EDGE ( 'NONE', *, *, #15329, .F. ) ;
#114476=VERTEX_POINT ( 'NONE', #19885 ) ;
#114477=ADVANCED_FACE ( 'NONE', ( #66280 ), #32215, .F. ) ;
#114478=CARTESIAN_POINT ( 'NONE',  ( 26.99999999999980105, -13.06887692260767331, 4.000000000000000000 ) ) ;
#114480=VERTEX_POINT ( 'NONE', #64130 ) ;
#114481=PLANE ( 'NONE',  #74090 ) ;
#114482=CARTESIAN_POINT ( 'NONE',  ( -16.82816939922341248, -8.240707523384195099, 4.000000000000000000 ) ) ;
#114483=LINE ( 'NONE', #15164, #53358 ) ;
#114485=EDGE_CURVE ( 'NONE', #42223, #23228, #108296, .T. ) ;
#114487=DIRECTION ( 'NONE',  ( -0.7071067811865487940, 0.7071067811865463515, -0.000000000000000000 ) ) ;
#114488=FACE_OUTER_BOUND ( 'NONE', #141163, .T. ) ;
#114489=PLANE ( 'NONE',  #125844 ) ;
#114491=FACE_OUTER_BOUND ( 'NONE', #64656, .T. ) ;
#114492=DIRECTION ( 'NONE',  ( 0.7071067811865486830, -0.7071067811865464625, -0.000000000000000000 ) ) ;
#114494=LINE ( 'NONE', #15173, #3579 ) ;
#114496=EDGE_CURVE ( 'NONE', #9195, #41509, #88752, .T. ) ;
#114497=ADVANCED_FACE ( 'NONE', ( #33662 ), #98872, .F. ) ;
#114498=VECTOR ( 'NONE', #128423, 1000.000000000000000 ) ;
#114499=ORIENTED_EDGE ( 'NONE', *, *, #16898, .T. ) ;
#114500=ORIENTED_EDGE ( 'NONE', *, *, #35385, .F. ) ;
#114503=( BOUNDED_CURVE ( )  B_SPLINE_CURVE ( 3, ( #67602, #123, #111793, #110328 ),
 .UNSPECIFIED., .F., .T. ) 
 B_SPLINE_CURVE_WITH_KNOTS ( ( 4, 4 ),
 ( 0.6873533248919956318, 0.6988790395524699939 ),
 .UNSPECIFIED. ) 
 CURVE ( )  GEOMETRIC_REPRESENTATION_ITEM ( )  RATIONAL_B_SPLINE_CURVE ( ( 1.000000000000000000, 0.9999889298557675943, 0.9999889298557675943, 1.000000000000000000 ) ) 
 REPRESENTATION_ITEM ( '' )  );
#114504=ORIENTED_EDGE ( 'NONE', *, *, #63708, .T. ) ;
#114505=VECTOR ( 'NONE', #142331, 1000.000000000000000 ) ;
#114506=EDGE_CURVE ( 'NONE', #55578, #109227, #13998, .T. ) ;
#114508=EDGE_CURVE ( 'NONE', #31895, #11167, #26336, .T. ) ;
#114509=DIRECTION ( 'NONE',  ( 0.7071067811865487940, 0.7071067811865463515, -0.000000000000000000 ) ) ;
#114510=ORIENTED_EDGE ( 'NONE', *, *, #4630, .F. ) ;
#114511=DIRECTION ( 'NONE',  ( 0.7071067811865487940, -0.7071067811865463515, 0.000000000000000000 ) ) ;
#114513=ADVANCED_FACE ( 'NONE', ( #112624 ), #69139, .F. ) ;
#114515=AXIS2_PLACEMENT_3D ( 'NONE', #53294, #117119, #85930 ) ;
#114516=VERTEX_POINT ( 'NONE', #134391 ) ;
#114517=ORIENTED_EDGE ( 'NONE', *, *, #35661, .F. ) ;
#114518=CARTESIAN_POINT ( 'NONE',  ( -4.499999999999957367, -4.912538124160707120, 4.000000000000000000 ) ) ;
#114519=FACE_OUTER_BOUND ( 'NONE', #73029, .T. ) ;
#114520=DIRECTION ( 'NONE',  ( -0.000000000000000000, 0.000000000000000000, 1.000000000000000000 ) ) ;
#114521=EDGE_CURVE ( 'NONE', #31605, #72597, #58303, .T. ) ;
#114522=EDGE_LOOP ( 'NONE', ( #126436, #78920, #125674, #44478 ) ) ;
#114523=ORIENTED_EDGE ( 'NONE', *, *, #7270, .T. ) ;
#114524=VERTEX_POINT ( 'NONE', #984 ) ;
#114525=CARTESIAN_POINT ( 'NONE',  ( -69.18398860626899705, 28.73617430169835529, 5.000000000000000000 ) ) ;
#114527=EDGE_CURVE ( 'NONE', #87598, #96265, #111925, .T. ) ;
#114531=VECTOR ( 'NONE', #36872, 999.9999999999998863 ) ;
#114532=CARTESIAN_POINT ( 'NONE',  ( 19.05000000000000071, 3.174999999999997158, 4.000000000000000000 ) ) ;
#114533=EDGE_LOOP ( 'NONE', ( #106375, #32756, #61957 ) ) ;
#114536=CARTESIAN_POINT ( 'NONE',  ( 2.816011393730999401, 28.73617430169785436, 5.000000000000000000 ) ) ;
#114537=ORIENTED_EDGE ( 'NONE', *, *, #33496, .T. ) ;
#114538=ORIENTED_EDGE ( 'NONE', *, *, #89328, .F. ) ;
#114539=DIRECTION ( 'NONE',  ( -0.3543493200069162685, -0.000000000000000000, -0.9351131265310288487 ) ) ;
#114540=EDGE_CURVE ( 'NONE', #29743, #9910, #56864, .T. ) ;
#114541=CARTESIAN_POINT ( 'NONE',  ( -81.18398860626899705, 28.73617430169844056, 5.000000000000000000 ) ) ;
#114542=ORIENTED_EDGE ( 'NONE', *, *, #105500, .T. ) ;
#114543=DIRECTION ( 'NONE',  ( 0.6830127018922180770, -0.6830127018922204085, -0.2588190451025213501 ) ) ;
#114544=EDGE_CURVE ( 'NONE', #30609, #82053, #35092, .T. ) ;
#114545=FACE_OUTER_BOUND ( 'NONE', #28358, .T. ) ;
#114546=DIRECTION ( 'NONE',  ( -0.7071067811865487940, 0.7071067811865463515, 0.000000000000000000 ) ) ;
#114548=CARTESIAN_POINT ( 'NONE',  ( 21.29974487139158512, -27.71228299555221142, 4.000000000000000000 ) ) ;
#114549=CARTESIAN_POINT ( 'NONE',  ( 48.29974487139158867, -27.71228299555239971, 4.000000000000000000 ) ) ;
#114550=FACE_BOUND ( 'NONE', #120020, .T. ) ;
#114551=ORIENTED_EDGE ( 'NONE', *, *, #39889, .F. ) ;
#114553=CARTESIAN_POINT ( 'NONE',  ( -27.18398860626900060, 28.73617430169806042, 5.000000000000000000 ) ) ;
#114554=DIRECTION ( 'NONE',  ( -0.7071067811865486830, -0.7071067811865464625, 0.000000000000000000 ) ) ;
#114555=ORIENTED_EDGE ( 'NONE', *, *, #27205, .F. ) ;
#114556=CARTESIAN_POINT ( 'NONE',  ( 4.585192374791373204, 22.22500000000000142, 19.97188885935846869 ) ) ;
#114557=EDGE_LOOP ( 'NONE', ( #100249, #81715, #37902, #44724 ) ) ;
#114558=ORIENTED_EDGE ( 'NONE', *, *, #41366, .T. ) ;
#114559=ORIENTED_EDGE ( 'NONE', *, *, #27142, .F. ) ;
#114561=ORIENTED_EDGE ( 'NONE', *, *, #42689, .F. ) ;
#114562=LINE ( 'NONE', #15231, #15893 ) ;
#114563=DIRECTION ( 'NONE',  ( -0.7071067811865486830, 0.7071067811865464625, 0.000000000000000000 ) ) ;
#114564=DIRECTION ( 'NONE',  ( -0.7071067811865487940, 0.7071067811865463515, -0.000000000000000000 ) ) ;
#114565=EDGE_CURVE ( 'NONE', #22070, #17208, #79333, .T. ) ;
#114566=ORIENTED_EDGE ( 'NONE', *, *, #77569, .F. ) ;
#114567=LINE ( 'NONE', #134945, #483 ) ;
#114568=CARTESIAN_POINT ( 'NONE',  ( 34.49999999999975842, -7.535744391599426883, 4.994342998332164107 ) ) ;
#114569=DIRECTION ( 'NONE',  ( 0.7071067811865487940, 0.7071067811865463515, 0.000000000000000000 ) ) ;
#114570=LINE ( 'NONE', #5071, #141236 ) ;
#114571=CARTESIAN_POINT ( 'NONE',  ( 0.000000000000000000, 0.000000000000000000, 5.000000000000000000 ) ) ;
#114572=EDGE_CURVE ( 'NONE', #126032, #46388, #45268, .T. ) ;
#114573=DIRECTION ( 'NONE',  ( 0.7071067811865486830, -0.7071067811865464625, -0.000000000000000000 ) ) ;
#114574=VERTEX_POINT ( 'NONE', #113317 ) ;
#114575=ORIENTED_EDGE ( 'NONE', *, *, #57272, .T. ) ;
#114576=EDGE_LOOP ( 'NONE', ( #97003, #81855, #13269, #8591 ) ) ;
#114580=ORIENTED_EDGE ( 'NONE', *, *, #83682, .F. ) ;
#114581=FACE_OUTER_BOUND ( 'NONE', #122761, .T. ) ;
#114582=ADVANCED_FACE ( 'NONE', ( #133671 ), #34353, .T. ) ;
#114583=DIRECTION ( 'NONE',  ( 0.7071067811865486830, -0.7071067811865464625, -0.000000000000000000 ) ) ;
#114584=ORIENTED_EDGE ( 'NONE', *, *, #116326, .T. ) ;
#114586=ORIENTED_EDGE ( 'NONE', *, *, #71671, .F. ) ;
#114588=AXIS2_PLACEMENT_3D ( 'NONE', #84577, #116476, #38918 ) ;
#114589=PLANE ( 'NONE',  #68230 ) ;
#114591=ORIENTED_EDGE ( 'NONE', *, *, #71247, .F. ) ;
#114593=DIRECTION ( 'NONE',  ( 0.000000000000000000, -1.000000000000000000, 0.000000000000000000 ) ) ;
#114597=ORIENTED_EDGE ( 'NONE', *, *, #106858, .T. ) ;
#114598=CARTESIAN_POINT ( 'NONE',  ( 57.48921356237308800, -27.52281430457095368, 5.000000000000000000 ) ) ;
#114599=ORIENTED_EDGE ( 'NONE', *, *, #116414, .T. ) ;
#114600=CARTESIAN_POINT ( 'NONE',  ( -39.48921356237310221, -27.52281430457082934, 5.000000000000000000 ) ) ;
#114603=CARTESIAN_POINT ( 'NONE',  ( -32.99451991528749062, 28.92564299267960948, 4.000000000000000000 ) ) ;
#114604=ORIENTED_EDGE ( 'NONE', *, *, #79035, .T. ) ;
#114607=ADVANCED_FACE ( 'NONE', ( #78576 ), #92276, .F. ) ;
#114608=VECTOR ( 'NONE', #32648, 1000.000000000000000 ) ;
#114609=VECTOR ( 'NONE', #52291, 1000.000000000000227 ) ;
#114610=DIRECTION ( 'NONE',  ( -0.000000000000000000, -0.000000000000000000, 1.000000000000000000 ) ) ;
#114611=LINE ( 'NONE', #126225, #7439 ) ;
#114612=EDGE_LOOP ( 'NONE', ( #70152, #98708, #16876, #96264 ) ) ;
#114613=DIRECTION ( 'NONE',  ( 0.000000000000000000, 1.000000000000000000, 0.000000000000000000 ) ) ;
#114614=CARTESIAN_POINT ( 'NONE',  ( 19.82816939922337696, -17.24070752338412049, 4.000000000000000000 ) ) ;
#114615=VERTEX_POINT ( 'NONE', #123533 ) ;
#114616=DIRECTION ( 'NONE',  ( 0.7071067811865486830, 0.7071067811865463515, 0.000000000000000000 ) ) ;
#114617=ORIENTED_EDGE ( 'NONE', *, *, #2709, .F. ) ;
#114618=ADVANCED_FACE ( 'NONE', ( #37202 ), #24196, .F. ) ;
#114619=VERTEX_POINT ( 'NONE', #80039 ) ;
#114620=LINE ( 'NONE', #5122, #42643 ) ;
#114621=PLANE ( 'NONE',  #131721 ) ;
#114623=DIRECTION ( 'NONE',  ( -0.7071067811865486830, -0.7071067811865464625, 0.000000000000000000 ) ) ;
#114624=VECTOR ( 'NONE', #108580, 1000.000000000000000 ) ;
#114625=CARTESIAN_POINT ( 'NONE',  ( -21.48921356237309155, -27.52281430457070499, 5.000000000000000000 ) ) ;
#114626=VECTOR ( 'NONE', #85168, 1000.000000000000000 ) ;
#114628=FACE_OUTER_BOUND ( 'NONE', #87759, .T. ) ;
#114629=ORIENTED_EDGE ( 'NONE', *, *, #62325, .T. ) ;
#114631=CARTESIAN_POINT ( 'NONE',  ( -5.563198967791673333, -12.74070752338415247, 9.898150129686387189 ) ) ;
#114632=FACE_OUTER_BOUND ( 'NONE', #38320, .T. ) ;
#114633=DIRECTION ( 'NONE',  ( -0.7071067811865487940, 0.7071067811865463515, 0.000000000000000000 ) ) ;
#114634=DIRECTION ( 'NONE',  ( -0.000000000000000000, 0.000000000000000000, 1.000000000000000000 ) ) ;
#114635=LINE ( 'NONE', #103745, #86437 ) ;
#114638=DIRECTION ( 'NONE',  ( -0.6830127018922180770, -0.6830127018922204085, -0.2588190451025213501 ) ) ;
#114639=ORIENTED_EDGE ( 'NONE', *, *, #6960, .T. ) ;
#114640=VERTEX_POINT ( 'NONE', #124213 ) ;
#114641=ORIENTED_EDGE ( 'NONE', *, *, #37987, .F. ) ;
#114643=ORIENTED_EDGE ( 'NONE', *, *, #89746, .F. ) ;
#114644=ORIENTED_EDGE ( 'NONE', *, *, #91186, .T. ) ;
#114645=ORIENTED_EDGE ( 'NONE', *, *, #1487, .T. ) ;
#114646=CARTESIAN_POINT ( 'NONE',  ( -16.21498419724179740, -3.740707523384238176, 15.76143240460120154 ) ) ;
#114647=CARTESIAN_POINT ( 'NONE',  ( -32.99999999999977263, 12.25461709320617842, -10.07315571508704544 ) ) ;
#114648=ORIENTED_EDGE ( 'NONE', *, *, #103325, .F. ) ;
#114649=DIRECTION ( 'NONE',  ( 1.000000000000000000, -0.000000000000000000, -0.000000000000000000 ) ) ;
#114650=CARTESIAN_POINT ( 'NONE',  ( -11.99451991528749417, 28.92564299267946382, 4.000000000000000000 ) ) ;
#114654=EDGE_CURVE ( 'NONE', #101750, #112039, #114046, .T. ) ;
#114655=FACE_OUTER_BOUND ( 'NONE', #135845, .T. ) ;
#114657=CARTESIAN_POINT ( 'NONE',  ( 10.35824297541133099, 15.75929247661555088, 19.34181609438697080 ) ) ;
#114659=DIRECTION ( 'NONE',  ( 0.7071067811865487940, 0.7071067811865463515, 0.000000000000000000 ) ) ;
#114660=LINE ( 'NONE', #69056, #95521 ) ;
#114661=LINE ( 'NONE', #113967, #112947 ) ;
#114663=CARTESIAN_POINT ( 'NONE',  ( -28.49999999999980460, 13.56627193232212392, -10.57019076586074924 ) ) ;
#114664=ADVANCED_FACE ( 'NONE', ( #128507 ), #29176, .F. ) ;
#114666=VERTEX_POINT ( 'NONE', #127053 ) ;
#114669=EDGE_CURVE ( 'NONE', #45045, #116840, #16884, .T. ) ;
#114670=EDGE_LOOP ( 'NONE', ( #72073, #62947, #118933, #98344 ) ) ;
#114671=EDGE_LOOP ( 'NONE', ( #102368, #93495, #72874, #40908 ) ) ;
#114672=DIRECTION ( 'NONE',  ( 0.7071067811865487940, -0.7071067811865463515, 0.000000000000000000 ) ) ;
#114673=ADVANCED_FACE ( 'NONE', ( #60413 ), #29875, .F. ) ;
#114674=PLANE ( 'NONE',  #68764 ) ;
#114675=EDGE_LOOP ( 'NONE', ( #25057, #68297, #67350, #31184 ) ) ;
#114676=EDGE_CURVE ( 'NONE', #118592, #67057, #103851, .T. ) ;
#114678=LINE ( 'NONE', #15346, #28421 ) ;
#114679=CARTESIAN_POINT ( 'NONE',  ( 2.816011393730999401, 28.73617430169785436, 5.000000000000000000 ) ) ;
#114682=EDGE_CURVE ( 'NONE', #46293, #84665, #82867, .T. ) ;
#114683=DIRECTION ( 'NONE',  ( -0.7071067811865486830, -0.7071067811865464625, 0.000000000000000000 ) ) ;
#114684=VERTEX_POINT ( 'NONE', #118309 ) ;
#114685=FACE_OUTER_BOUND ( 'NONE', #136260, .T. ) ;
#114686=LINE ( 'NONE', #137190, #117106 ) ;
#114687=EDGE_CURVE ( 'NONE', #92319, #15951, #5961, .T. ) ;
#114688=LINE ( 'NONE', #95083, #134423 ) ;
#114689=ORIENTED_EDGE ( 'NONE', *, *, #114431, .T. ) ;
#114690=ADVANCED_FACE ( 'NONE', ( #72746 ), #62541, .F. ) ;
#114691=EDGE_LOOP ( 'NONE', ( #81306, #106428, #101278, #36881 ) ) ;
#114692=DIRECTION ( 'NONE',  ( -0.6830127018922180770, -0.6830127018922204085, -0.2588190451025213501 ) ) ;
#114693=CARTESIAN_POINT ( 'NONE',  ( 5.483345613589513334, 22.22500000000000142, 4.500000000000000888 ) ) ;
#114694=DIRECTION ( 'NONE',  ( -0.6830127018922181881, 0.6830127018922202975, -0.2588190451025214056 ) ) ;
#114695=ADVANCED_FACE ( 'NONE', ( #61834 ), #115429, .F. ) ;
#114696=VECTOR ( 'NONE', #132202, 1000.000000000000000 ) ;
#114698=VECTOR ( 'NONE', #138802, 1000.000000000000000 ) ;
#114699=LINE ( 'NONE', #127005, #136841 ) ;
#114700=CARTESIAN_POINT ( 'NONE',  ( -1.828169399223516400, 6.759292476615651246, 4.000000000000000000 ) ) ;
#114701=ORIENTED_EDGE ( 'NONE', *, *, #24105, .T. ) ;
#114702=ORIENTED_EDGE ( 'NONE', *, *, #136119, .T. ) ;
#114703=CARTESIAN_POINT ( 'NONE',  ( -4.499999999999962697, 13.46639925780213076, 5.000000000000000000 ) ) ;
#114704=EDGE_LOOP ( 'NONE', ( #22313, #68095, #104942, #134050 ) ) ;
#114705=VECTOR ( 'NONE', #75813, 1000.000000000000000 ) ;
#114707=ORIENTED_EDGE ( 'NONE', *, *, #30388, .F. ) ;
#114708=LINE ( 'NONE', #6626, #122360 ) ;
#114709=ADVANCED_FACE ( 'NONE', ( #106711 ), #105305, .F. ) ;
#114710=CARTESIAN_POINT ( 'NONE',  ( -10.49999999999992539, 19.08746187583905751, 4.000000000000000000 ) ) ;
#114711=FACE_BOUND ( 'NONE', #32342, .T. ) ;
#114712=CARTESIAN_POINT ( 'NONE',  ( 45.18398860626900415, 28.73617430169818832, 5.000000000000000000 ) ) ;
#114713=CARTESIAN_POINT ( 'NONE',  ( -11.15466569459995583, 22.22500000000000142, 14.00746825007390406 ) ) ;
#114715=LINE ( 'NONE', #135785, #129120 ) ;
#114717=VERTEX_POINT ( 'NONE', #50946 ) ;
#114718=DIRECTION ( 'NONE',  ( 0.7071067811865486830, -0.7071067811865464625, -0.000000000000000000 ) ) ;
#114722=VECTOR ( 'NONE', #82599, 1000.000000000000000 ) ;
#114723=ORIENTED_EDGE ( 'NONE', *, *, #91229, .T. ) ;
#114725=ORIENTED_EDGE ( 'NONE', *, *, #35653, .T. ) ;
#114726=VECTOR ( 'NONE', #59359, 1000.000000000000000 ) ;
#114727=LINE ( 'NONE', #80720, #113806 ) ;
#114728=FACE_OUTER_BOUND ( 'NONE', #39659, .T. ) ;
#114729=EDGE_CURVE ( 'NONE', #137509, #103304, #51661, .T. ) ;
#114730=VERTEX_POINT ( 'NONE', #21153 ) ;
#114731=CARTESIAN_POINT ( 'NONE',  ( -24.09843580608222169, 11.25929247661560240, 10.79108189686401431 ) ) ;
#114732=VECTOR ( 'NONE', #117129, 1000.000000000000000 ) ;
#114733=FACE_OUTER_BOUND ( 'NONE', #105111, .T. ) ;
#114734=EDGE_CURVE ( 'NONE', #86215, #26526, #87841, .T. ) ;
#114736=CARTESIAN_POINT ( 'NONE',  ( -25.88982677111770414, -22.22500000000000142, 4.785647885939355639 ) ) ;
#114737=CARTESIAN_POINT ( 'NONE',  ( -0.4892135623730947680, -27.52281430457055578, 5.000000000000000000 ) ) ;
#114738=CARTESIAN_POINT ( 'NONE',  ( -36.18398860626899705, 28.73617430169812437, 5.000000000000000000 ) ) ;
#114739=EDGE_LOOP ( 'NONE', ( #97647, #81588, #113852, #76091, #131153 ) ) ;
#114740=ORIENTED_EDGE ( 'NONE', *, *, #112108, .T. ) ;
#114741=CARTESIAN_POINT ( 'NONE',  ( -17.99451991528748351, 28.92564299267950645, 4.000000000000000000 ) ) ;
#114742=CARTESIAN_POINT ( 'NONE',  ( 48.18398860626899705, 28.73617430169820608, 5.000000000000000000 ) ) ;
#114743=ORIENTED_EDGE ( 'NONE', *, *, #54752, .T. ) ;
#114744=EDGE_LOOP ( 'NONE', ( #90036, #142060, #68876, #142877 ) ) ;
#114745=VERTEX_POINT ( 'NONE', #64669 ) ;
#114747=EDGE_LOOP ( 'NONE', ( #13665, #111177, #136316, #110480 ) ) ;
#114751=CARTESIAN_POINT ( 'NONE',  ( 34.92499999999998295, -0.1833456135895417671, 4.500000000000000888 ) ) ;
#114752=ORIENTED_EDGE ( 'NONE', *, *, #35708, .F. ) ;
#114753=DIRECTION ( 'NONE',  ( 0.7071067811865486830, -0.7071067811865464625, -0.000000000000000000 ) ) ;
#114755=DIRECTION ( 'NONE',  ( -0.000000000000000000, 0.3543493200069153248, 0.9351131265310292928 ) ) ;
#114757=ORIENTED_EDGE ( 'NONE', *, *, #92244, .T. ) ;
#114758=DIRECTION ( 'NONE',  ( 0.6830127018922181881, 0.6830127018922202975, -0.2588190451025214056 ) ) ;
#114760=PLANE ( 'NONE',  #75047 ) ;
#114761=LINE ( 'NONE', #104626, #26121 ) ;
#114762=EDGE_CURVE ( 'NONE', #130905, #92017, #10265, .T. ) ;
#114763=DIRECTION ( 'NONE',  ( 1.000000000000000000, 0.000000000000000000, 0.000000000000000000 ) ) ;
#114764=EDGE_LOOP ( 'NONE', ( #23852, #11229, #49378, #110054 ) ) ;
#114765=DIRECTION ( 'NONE',  ( 0.7071067811865487940, 0.7071067811865463515, -0.000000000000000000 ) ) ;
#114767=ADVANCED_FACE ( 'NONE', ( #65411 ), #75550, .F. ) ;
#114768=CARTESIAN_POINT ( 'NONE',  ( 2.915086768062360889, -12.74070752338415602, 18.74364270924355225 ) ) ;
#114770=DIRECTION ( 'NONE',  ( -0.6830127018922181881, 0.6830127018922202975, -0.2588190451025214056 ) ) ;
#114773=CARTESIAN_POINT ( 'NONE',  ( 28.49999999999980460, -12.08601207473286543, -10.46905243149100961 ) ) ;
#114774=( BOUNDED_CURVE ( )  B_SPLINE_CURVE ( 3, ( #76712, #102003, #46965, #111439 ),
 .UNSPECIFIED., .F., .T. ) 
 B_SPLINE_CURVE_WITH_KNOTS ( ( 4, 4 ),
 ( 1.901594255663603183, 1.933014472006576945 ),
 .UNSPECIFIED. ) 
 CURVE ( )  GEOMETRIC_REPRESENTATION_ITEM ( )  RATIONAL_B_SPLINE_CURVE ( ( 1.000000000000000000, 0.9999177325257866400, 0.9999177325257866400, 1.000000000000000000 ) ) 
 REPRESENTATION_ITEM ( '' )  );
#114775=CARTESIAN_POINT ( 'NONE',  ( 17.11162361894747619, 9.759292476615614831, 17.35367589129208810 ) ) ;
#114776=DIRECTION ( 'NONE',  ( 0.7071067811865486830, -0.7071067811865464625, -0.000000000000000000 ) ) ;
#114777=CARTESIAN_POINT ( 'NONE',  ( 71.99451991528749772, 28.92564299267988304, 4.000000000000000000 ) ) ;
#114778=ORIENTED_EDGE ( 'NONE', *, *, #121883, .F. ) ;
#114779=EDGE_CURVE ( 'NONE', #132371, #110801, #54525, .T. ) ;
#114780=VERTEX_POINT ( 'NONE', #74860 ) ;
#114781=PLANE ( 'NONE',  #61101 ) ;
#114782=PRODUCT_DEFINITION ( 'UNKNOWN', '', #121211, #128474 ) ;
#114784=AXIS2_PLACEMENT_3D ( 'NONE', #15626, #71497, #77325 ) ;
#114786=LINE ( 'NONE', #48863, #143380 ) ;
#114787=DIRECTION ( 'NONE',  ( -0.6830127018922180770, -0.6830127018922204085, -0.2588190451025213501 ) ) ;
#114788=FACE_OUTER_BOUND ( 'NONE', #134313, .T. ) ;
#114789=AXIS2_PLACEMENT_3D ( 'NONE', #128282, #116675, #127559 ) ;
#114790=VERTEX_POINT ( 'NONE', #77002 ) ;
#114791=PLANE ( 'NONE',  #51621 ) ;
#114792=CARTESIAN_POINT ( 'NONE',  ( -69.18398860626899705, 28.73617430169835529, 5.000000000000000000 ) ) ;
#114794=EDGE_CURVE ( 'NONE', #74021, #99505, #30630, .T. ) ;
#114795=CARTESIAN_POINT ( 'NONE',  ( -0.7586007421979610310, 21.72500000000000853, 5.000000000000000000 ) ) ;
#114797=CARTESIAN_POINT ( 'NONE',  ( -34.42500000000001137, -0.02281430457058350458, 5.000000000000000000 ) ) ;
#114798=ORIENTED_EDGE ( 'NONE', *, *, #97011, .T. ) ;
#114799=VECTOR ( 'NONE', #142326, 999.9999999999998863 ) ;
#114801=VERTEX_POINT ( 'NONE', #109589 ) ;
#114802=DIRECTION ( 'NONE',  ( -0.000000000000000000, -0.3543493200069152693, 0.9351131265310292928 ) ) ;
#114803=CARTESIAN_POINT ( 'NONE',  ( 5.999999999999960920, -15.41253812416059787, 4.000000000000000000 ) ) ;
#114804=LINE ( 'NONE', #62613, #83587 ) ;
#114805=DIRECTION ( 'NONE',  ( 0.7071067811865486830, -0.7071067811865464625, -0.000000000000000000 ) ) ;
#114806=CARTESIAN_POINT ( 'NONE',  ( -34.75611968250420603, -16.29434930147576921, 4.955485411084901592 ) ) ;
#114808=ORIENTED_EDGE ( 'NONE', *, *, #60928, .F. ) ;
#114809=DIRECTION ( 'NONE',  ( -0.6830127018922181881, 0.6830127018922202975, -0.2588190451025214056 ) ) ;
#114810=PLANE ( 'NONE',  #137187 ) ;
#114811=FACE_OUTER_BOUND ( 'NONE', #16332, .T. ) ;
#114812=VECTOR ( 'NONE', #53940, 1000.000000000000000 ) ;
#114813=FACE_OUTER_BOUND ( 'NONE', #63107, .T. ) ;
#114815=VECTOR ( 'NONE', #31440, 1000.000000000000000 ) ;
#114816=EDGE_CURVE ( 'NONE', #39099, #6138, #21866, .T. ) ;
#114818=ORIENTED_EDGE ( 'NONE', *, *, #33697, .F. ) ;
#114819=VERTEX_POINT ( 'NONE', #119036 ) ;
#114822=EDGE_CURVE ( 'NONE', #143096, #143231, #86434, .T. ) ;
#114824=LINE ( 'NONE', #139508, #43896 ) ;
#114825=LINE ( 'NONE', #14099, #86814 ) ;
#114826=ADVANCED_FACE ( 'NONE', ( #63280 ), #8110, .T. ) ;
#114827=VECTOR ( 'NONE', #3549, 1000.000000000000227 ) ;
#114828=EDGE_LOOP ( 'NONE', ( #143156, #138472, #98520, #59859 ) ) ;
#114829=EDGE_CURVE ( 'NONE', #125405, #25399, #142936, .T. ) ;
#114830=EDGE_CURVE ( 'NONE', #33874, #92295, #96539, .T. ) ;
#114834=DIRECTION ( 'NONE',  ( 0.6830127018922181881, 0.6830127018922202975, -0.2588190451025214056 ) ) ;
#114835=ORIENTED_EDGE ( 'NONE', *, *, #87128, .F. ) ;
#114837=LINE ( 'NONE', #12158, #123356 ) ;
#114838=DIRECTION ( 'NONE',  ( 0.7071067811865487940, 0.7071067811865463515, 0.000000000000000000 ) ) ;
#114839=CARTESIAN_POINT ( 'NONE',  ( 18.51665438641032324, 22.22500000000000142, 4.500000000000000888 ) ) ;
#114840=ADVANCED_FACE ( 'NONE', ( #110281 ), #98013, .T. ) ;
#114842=EDGE_CURVE ( 'NONE', #30447, #82994, #32772, .T. ) ;
#114843=CARTESIAN_POINT ( 'NONE',  ( 26.29289321881327623, -6.740707523384216415, 5.000000000000000000 ) ) ;
#114846=DIRECTION ( 'NONE',  ( 0.7071067811865486830, -0.7071067811865464625, -0.000000000000000000 ) ) ;
#114847=LINE ( 'NONE', #96652, #114812 ) ;
#114848=DIRECTION ( 'NONE',  ( 0.6830127018922180770, -0.6830127018922204085, -0.2588190451025213501 ) ) ;
#114849=LINE ( 'NONE', #59807, #27565 ) ;
#114850=EDGE_CURVE ( 'NONE', #45393, #54270, #108132, .T. ) ;
#114851=VERTEX_POINT ( 'NONE', #141516 ) ;
#114852=ORIENTED_EDGE ( 'NONE', *, *, #19114, .T. ) ;
#114853=CARTESIAN_POINT ( 'NONE',  ( 33.48921356237309510, -27.52281430457078670, 5.000000000000000000 ) ) ;
#114854=LINE ( 'NONE', #39489, #44143 ) ;
#114857=ORIENTED_EDGE ( 'NONE', *, *, #94202, .T. ) ;
#114858=ORIENTED_EDGE ( 'NONE', *, *, #105798, .T. ) ;
#114859=EDGE_CURVE ( 'NONE', #86507, #118884, #97295, .T. ) ;
#114861=LINE ( 'NONE', #48943, #19038 ) ;
#114862=CARTESIAN_POINT ( 'NONE',  ( 30.18398860626900060, 28.73617430169808173, 5.000000000000000000 ) ) ;
#114863=ORIENTED_EDGE ( 'NONE', *, *, #86707, .T. ) ;
#114864=CARTESIAN_POINT ( 'NONE',  ( -21.28001967989390764, 0.7592924766157173044, 14.27032725228004040 ) ) ;
#114865=ORIENTED_EDGE ( 'NONE', *, *, #57801, .F. ) ;
#114867=ADVANCED_FACE ( 'NONE', ( #31332 ), #119723, .F. ) ;
#114868=DIRECTION ( 'NONE',  ( -0.7071067811865486830, -0.7071067811865464625, 0.000000000000000000 ) ) ;
#114870=FACE_BOUND ( 'NONE', #3577, .T. ) ;
#114871=DIRECTION ( 'NONE',  ( -0.7071067811865487940, 0.7071067811865463515, 0.000000000000000000 ) ) ;
#114872=LINE ( 'NONE', #17708, #18868 ) ;
#114873=DIRECTION ( 'NONE',  ( 0.7071067811865487940, 0.7071067811865463515, 0.000000000000000000 ) ) ;
#114876=EDGE_CURVE ( 'NONE', #7339, #32128, #120425, .T. ) ;
#114878=ORIENTED_EDGE ( 'NONE', *, *, #115859, .F. ) ;
#114883=CARTESIAN_POINT ( 'NONE',  ( -18.79333936457834753, 21.75929247661549937, 4.998822639870701856 ) ) ;
#114884=CARTESIAN_POINT ( 'NONE',  ( -36.18398860626899705, 28.73617430169812437, 5.000000000000000000 ) ) ;
#114885=CARTESIAN_POINT ( 'NONE',  ( -0.1839886062690032631, 28.73617430169787568, 5.000000000000000000 ) ) ;
#114887=CARTESIAN_POINT ( 'NONE',  ( -6.328169399223480873, -18.74070752338408852, 4.000000000000000000 ) ) ;
#114890=ADVANCED_FACE ( 'NONE', ( #93373 ), #137608, .F. ) ;
#114891=LINE ( 'NONE', #38804, #108248 ) ;
#114892=CARTESIAN_POINT ( 'NONE',  ( -33.29974487139158867, -27.71228299555229313, 4.000000000000000000 ) ) ;
#114893=CARTESIAN_POINT ( 'NONE',  ( -11.99999999999991118, -6.412538124160689357, 4.000000000000000000 ) ) ;
#114894=DIRECTION ( 'NONE',  ( -0.3543493200069162685, -0.000000000000000000, -0.9351131265310288487 ) ) ;
#114895=CARTESIAN_POINT ( 'NONE',  ( -14.99999999999989875, 8.966399257802175171, 5.000000000000000000 ) ) ;
#114897=DIRECTION ( 'NONE',  ( -0.7071067811865487940, 0.7071067811865463515, -0.000000000000000000 ) ) ;
#114898=LINE ( 'NONE', #26507, #58150 ) ;
#114899=ORIENTED_EDGE ( 'NONE', *, *, #95781, .T. ) ;
#114901=ORIENTED_EDGE ( 'NONE', *, *, #140086, .F. ) ;
#114902=EDGE_CURVE ( 'NONE', #106219, #12022, #38289, .T. ) ;
#114903=VERTEX_POINT ( 'NONE', #808 ) ;
#114905=ORIENTED_EDGE ( 'NONE', *, *, #95829, .T. ) ;
#114909=ORIENTED_EDGE ( 'NONE', *, *, #70080, .F. ) ;
#114910=FACE_OUTER_BOUND ( 'NONE', #85548, .T. ) ;
#114911=ORIENTED_EDGE ( 'NONE', *, *, #110419, .T. ) ;
#114912=DIRECTION ( 'NONE',  ( 0.6830127018922180770, -0.6830127018922204085, -0.2588190451025213501 ) ) ;
#114913=VECTOR ( 'NONE', #68694, 1000.000000000000000 ) ;
#114914=DIRECTION ( 'NONE',  ( -0.7071067811865486830, -0.7071067811865464625, 0.000000000000000000 ) ) ;
#114915=LINE ( 'NONE', #46168, #35508 ) ;
#114916=VERTEX_POINT ( 'NONE', #138311 ) ;
#114917=ORIENTED_EDGE ( 'NONE', *, *, #55217, .T. ) ;
#114919=CARTESIAN_POINT ( 'NONE',  ( -34.92500000000001137, -12.03857301832753102, 17.98374865626354335 ) ) ;
#114920=ORIENTED_EDGE ( 'NONE', *, *, #88611, .F. ) ;
#114921=CARTESIAN_POINT ( 'NONE',  ( -25.82816939922335209, -5.240707523384228850, 4.000000000000000000 ) ) ;
#114922=ORIENTED_EDGE ( 'NONE', *, *, #97188, .F. ) ;
#114923=EDGE_CURVE ( 'NONE', #62444, #139660, #82505, .T. ) ;
#114924=VERTEX_POINT ( 'NONE', #36156 ) ;
#114926=ORIENTED_EDGE ( 'NONE', *, *, #124486, .T. ) ;
#114927=DIRECTION ( 'NONE',  ( 0.3543493200069162685, -0.000000000000000000, -0.9351131265310288487 ) ) ;
#114928=CARTESIAN_POINT ( 'NONE',  ( 23.99999999999982947, 20.70535890316563155, 1.956823837851859871 ) ) ;
#114932=FACE_OUTER_BOUND ( 'NONE', #105799, .T. ) ;
#114933=VERTEX_POINT ( 'NONE', #58669 ) ;
#114934=CARTESIAN_POINT ( 'NONE',  ( -25.59167451900982826, -0.7407075233842735917, 14.76736230305374775 ) ) ;
#114936=CARTESIAN_POINT ( 'NONE',  ( 0.000000000000000000, 0.000000000000000000, 5.000000000000000000 ) ) ;
#114937=AXIS2_PLACEMENT_3D ( 'NONE', #18095, #129749, #129032 ) ;
#114938=CARTESIAN_POINT ( 'NONE',  ( 31.49999999999977973, -10.04351517176475106, -1.623559851933751075 ) ) ;
#114940=DIRECTION ( 'NONE',  ( 1.000000000000000000, 0.000000000000000000, 0.000000000000000000 ) ) ;
#114941=EDGE_LOOP ( 'NONE', ( #109, #47425, #29017, #21723 ) ) ;
#114942=ORIENTED_EDGE ( 'NONE', *, *, #99601, .T. ) ;
#114945=DIRECTION ( 'NONE',  ( 0.7071067811865487940, 0.7071067811865463515, 0.000000000000000000 ) ) ;
#114946=DIRECTION ( 'NONE',  ( 0.7071067811865486830, -0.7071067811865464625, -0.000000000000000000 ) ) ;
#114947=AXIS2_PLACEMENT_3D ( 'NONE', #142869, #8728, #63206 ) ;
#114948=CARTESIAN_POINT ( 'NONE',  ( 1.828169399223523284, 3.759292476615681888, 4.000000000000000000 ) ) ;
#114949=DIRECTION ( 'NONE',  ( -0.000000000000000000, -0.3543493200069152693, 0.9351131265310292928 ) ) ;
#114951=EDGE_CURVE ( 'NONE', #99187, #75880, #113696, .T. ) ;
#114954=CARTESIAN_POINT ( 'NONE',  ( -6.183988606268994381, 28.73617430169791476, 5.000000000000000000 ) ) ;
#114955=LINE ( 'NONE', #47647, #62890 ) ;
#114956=PLANE ( 'NONE',  #81233 ) ;
#114957=AXIS2_PLACEMENT_3D ( 'NONE', #21780, #97917, #130557 ) ;
#114959=CARTESIAN_POINT ( 'NONE',  ( 8.999999999999937828, -5.527737879153182377, -7.983877177622392907 ) ) ;
#114961=LINE ( 'NONE', #38179, #27502 ) ;
#114962=CARTESIAN_POINT ( 'NONE',  ( 34.92499999999998295, 22.22500000000000142, 4.500000000000000888 ) ) ;
#114963=VERTEX_POINT ( 'NONE', #125295 ) ;
#114964=AXIS2_PLACEMENT_3D ( 'NONE', #23060, #52841, #98512 ) ;
#114965=CARTESIAN_POINT ( 'NONE',  ( -24.18398860626899705, 28.73617430169804265, 5.000000000000000000 ) ) ;
#114966=CARTESIAN_POINT ( 'NONE',  ( 24.70710678118637560, -3.740707523384243505, 5.000000000000000000 ) ) ;
#114968=DIRECTION ( 'NONE',  ( -0.000000000000000000, 0.000000000000000000, 1.000000000000000000 ) ) ;
#114969=ORIENTED_EDGE ( 'NONE', *, *, #2589, .F. ) ;
#114970=CARTESIAN_POINT ( 'NONE',  ( 65.99451991528749772, 28.92564299267984396, 4.000000000000000000 ) ) ;
#114971=ORIENTED_EDGE ( 'NONE', *, *, #16310, .T. ) ;
#114972=PLANE ( 'NONE',  #103137 ) ;
#114973=AXIS2_PLACEMENT_3D ( 'NONE', #59008, #3803, #127049 ) ;
#114974=EDGE_CURVE ( 'NONE', #6620, #122713, #70248, .T. ) ;
#114976=DIRECTION ( 'NONE',  ( 0.6830127018922180770, -0.6830127018922204085, -0.2588190451025213501 ) ) ;
#114977=EDGE_CURVE ( 'NONE', #1511, #37150, #60052, .T. ) ;
#114978=CARTESIAN_POINT ( 'NONE',  ( -80.99451991528748351, 28.92564299267994699, 4.000000000000000000 ) ) ;
#114979=ORIENTED_EDGE ( 'NONE', *, *, #126495, .F. ) ;
#114981=CARTESIAN_POINT ( 'NONE',  ( 34.75611968250419892, -18.18706574529242204, 4.955485411084882941 ) ) ;
#114982=CARTESIAN_POINT ( 'NONE',  ( -20.24139925780189841, 21.72500000000000853, 5.000000000000000000 ) ) ;
#114983=ADVANCED_FACE ( 'NONE', ( #92638 ), #37584, .F. ) ;
#114984=DIRECTION ( 'NONE',  ( -0.7071067811865487940, 0.7071067811865463515, 0.000000000000000000 ) ) ;
#114985=VECTOR ( 'NONE', #76348, 1000.000000000000227 ) ;
#114988=LINE ( 'NONE', #47678, #63040 ) ;
#114989=ORIENTED_EDGE ( 'NONE', *, *, #61392, .F. ) ;
#114990=ADVANCED_FACE ( 'NONE', ( #29523 ), #129556, .F. ) ;
#114991=EDGE_CURVE ( 'NONE', #70329, #29685, #74502, .T. ) ;
#114992=DIRECTION ( 'NONE',  ( -0.000000000000000000, -0.3543493200069152693, 0.9351131265310292928 ) ) ;
#114993=EDGE_LOOP ( 'NONE', ( #41938, #109046, #3694, #86448 ) ) ;
#114995=DIRECTION ( 'NONE',  ( -0.7071067811865487940, 0.7071067811865463515, 0.000000000000000000 ) ) ;
#114996=CARTESIAN_POINT ( 'NONE',  ( -14.99451991528749595, 28.92564299267948513, 4.000000000000000000 ) ) ;
#114997=DIRECTION ( 'NONE',  ( 0.7071067811865486830, -0.7071067811865464625, -0.000000000000000000 ) ) ;
#114998=ORIENTED_EDGE ( 'NONE', *, *, #132246, .F. ) ;
#114999=LINE ( 'NONE', #15678, #134558 ) ;
#115001=VECTOR ( 'NONE', #84091, 1000.000000000000227 ) ;
#115002=ADVANCED_FACE ( 'NONE', ( #139028 ), #39734, .F. ) ;
#115004=EDGE_CURVE ( 'NONE', #28808, #83728, #85331, .T. ) ;
#115005=CARTESIAN_POINT ( 'NONE',  ( 3.183988606268992161, 28.73617430169789699, 5.000000000000000000 ) ) ;
#115006=LINE ( 'NONE', #114330, #116884 ) ;
#115008=CARTESIAN_POINT ( 'NONE',  ( 54.29974487139159578, -27.71228299555243879, 4.000000000000000000 ) ) ;
#115009=CARTESIAN_POINT ( 'NONE',  ( -5.999999999999963585, 20.96639925780204905, 5.000000000000000000 ) ) ;
#115011=AXIS2_PLACEMENT_3D ( 'NONE', #9485, #58618, #54478 ) ;
#115013=VECTOR ( 'NONE', #98665, 1000.000000000000000 ) ;
#115015=ORIENTED_EDGE ( 'NONE', *, *, #88668, .F. ) ;
#115016=ORIENTED_EDGE ( 'NONE', *, *, #63323, .F. ) ;
#115017=AXIS2_PLACEMENT_3D ( 'NONE', #126606, #27297, #64773 ) ;
#115019=ORIENTED_EDGE ( 'NONE', *, *, #28839, .F. ) ;
#115020=EDGE_CURVE ( 'NONE', #22078, #112797, #72385, .T. ) ;
#115021=FACE_OUTER_BOUND ( 'NONE', #126281, .T. ) ;
#115022=CIRCLE ( 'NONE', #138248, 5.968999999999998529 ) ;
#115023=LINE ( 'NONE', #58604, #142930 ) ;
#115024=CARTESIAN_POINT ( 'NONE',  ( 21.29974487139158512, -27.71228299555221142, 4.000000000000000000 ) ) ;
#115026=DIRECTION ( 'NONE',  ( 0.7071067811865487940, 0.7071067811865463515, 0.000000000000000000 ) ) ;
#115027=EDGE_LOOP ( 'NONE', ( #49495, #38114, #26110, #98218 ) ) ;
#115030=CARTESIAN_POINT ( 'NONE',  ( -17.99451991528748351, 28.92564299267950645, 4.000000000000000000 ) ) ;
#115032=ORIENTED_EDGE ( 'NONE', *, *, #4276, .T. ) ;
#115033=PLANE ( 'NONE',  #55892 ) ;
#115034=LINE ( 'NONE', #104161, #107971 ) ;
#115035=EDGE_CURVE ( 'NONE', #3179, #108745, #51310, .T. ) ;
#115036=CARTESIAN_POINT ( 'NONE',  ( 8.700255128608413102, -27.71228299555199825, 4.000000000000000000 ) ) ;
#115037=ORIENTED_EDGE ( 'NONE', *, *, #41847, .T. ) ;
#115038=ORIENTED_EDGE ( 'NONE', *, *, #81689, .F. ) ;
#115039=CARTESIAN_POINT ( 'NONE',  ( 24.70701326429286482, -21.74070752338406365, 4.999753212805220670 ) ) ;
#115040=CARTESIAN_POINT ( 'NONE',  ( -21.18398860626899349, 28.73617430169802134, 5.000000000000000000 ) ) ;
#115041=DIRECTION ( 'NONE',  ( 0.7071067811865486830, -0.7071067811865464625, -0.000000000000000000 ) ) ;
#115042=VECTOR ( 'NONE', #131361, 999.9999999999998863 ) ;
#115043=ADVANCED_FACE ( 'NONE', ( #9168 ), #73081, .F. ) ;
#115047=ADVANCED_FACE ( 'NONE', ( #28121 ), #117234, .F. ) ;
#115048=AXIS2_PLACEMENT_3D ( 'NONE', #37917, #14714, #58990 ) ;
#115049=EDGE_LOOP ( 'NONE', ( #91171, #127951, #24890, #126796 ) ) ;
#115050=ORIENTED_EDGE ( 'NONE', *, *, #118062, .F. ) ;
#115051=DIRECTION ( 'NONE',  ( 0.7071067811865486830, -0.7071067811865464625, -0.000000000000000000 ) ) ;
#115052=ORIENTED_EDGE ( 'NONE', *, *, #8183, .T. ) ;
#115053=VECTOR ( 'NONE', #36777, 1000.000000000000000 ) ;
#115054=ADVANCED_FACE ( 'NONE', ( #62188 ), #127419, .F. ) ;
#115055=DIRECTION ( 'NONE',  ( 0.7071067811865487940, 0.7071067811865463515, 0.000000000000000000 ) ) ;
#115058=FACE_OUTER_BOUND ( 'NONE', #64732, .T. ) ;
#115059=DIRECTION ( 'NONE',  ( 0.7071067811865487940, 0.7071067811865463515, 0.000000000000000000 ) ) ;
#115060=VECTOR ( 'NONE', #140514, 1000.000000000000000 ) ;
#115061=PLANE ( 'NONE',  #83170 ) ;
#115063=ORIENTED_EDGE ( 'NONE', *, *, #55046, .F. ) ;
#115064=LINE ( 'NONE', #105625, #118848 ) ;
#115065=CARTESIAN_POINT ( 'NONE',  ( -12.18398860626900060, 28.73617430169795739, 5.000000000000000000 ) ) ;
#115066=VECTOR ( 'NONE', #138288, 1000.000000000000000 ) ;
#115067=ORIENTED_EDGE ( 'NONE', *, *, #62356, .F. ) ;
#115068=LINE ( 'NONE', #61484, #24999 ) ;
#115069=VERTEX_POINT ( 'NONE', #107795 ) ;
#115070=ORIENTED_EDGE ( 'NONE', *, *, #122230, .T. ) ;
#115071=CARTESIAN_POINT ( 'NONE',  ( 0.000000000000000000, 0.000000000000000000, 5.000000000000000000 ) ) ;
#115072=ORIENTED_EDGE ( 'NONE', *, *, #30115, .T. ) ;
#115073=ORIENTED_EDGE ( 'NONE', *, *, #8865, .T. ) ;
#115075=ORIENTED_EDGE ( 'NONE', *, *, #36012, .F. ) ;
#115076=CARTESIAN_POINT ( 'NONE',  ( 23.93182425469048979, -0.2601698552150336075, 4.222180570310123393 ) ) ;
#115078=VECTOR ( 'NONE', #3785, 1000.000000000000227 ) ;
#115080=CARTESIAN_POINT ( 'NONE',  ( 0.000000000000000000, 0.000000000000000000, 5.000000000000000000 ) ) ;
#115081=ADVANCED_FACE ( 'NONE', ( #84646 ), #140440, .F. ) ;
#115082=LINE ( 'NONE', #135475, #43581 ) ;
#115083=FACE_OUTER_BOUND ( 'NONE', #89091, .T. ) ;
#115084=DIRECTION ( 'NONE',  ( -0.7071067811865486830, -0.7071067811865464625, 0.000000000000000000 ) ) ;
#115085=CARTESIAN_POINT ( 'NONE',  ( -14.92733143757284786, -1.141545485034857643, 4.000000000000000000 ) ) ;
#115086=PLANE ( 'NONE',  #58610 ) ;
#115088=PLANE ( 'NONE',  #123878 ) ;
#115089=VERTEX_POINT ( 'NONE', #139764 ) ;
#115090=CARTESIAN_POINT ( 'NONE',  ( -33.32816939922329880, -15.74070752338412404, 4.000000000000000000 ) ) ;
#115092=ORIENTED_EDGE ( 'NONE', *, *, #14618, .F. ) ;
#115094=DIRECTION ( 'NONE',  ( -0.7071067811865486830, -0.7071067811865464625, 0.000000000000000000 ) ) ;
#115096=CARTESIAN_POINT ( 'NONE',  ( -72.48921356237309510, -27.52281430457106026, 5.000000000000000000 ) ) ;
#115097=EDGE_CURVE ( 'NONE', #90471, #29177, #6303, .T. ) ;
#115098=CARTESIAN_POINT ( 'NONE',  ( 36.48921356237310221, -27.52281430457080802, 5.000000000000000000 ) ) ;
#115099=CARTESIAN_POINT ( 'NONE',  ( -41.99451991528749062, 28.92564299267967343, 4.000000000000000000 ) ) ;
#115100=EDGE_LOOP ( 'NONE', ( #86763, #97386, #41549, #48241 ) ) ;
#115101=EDGE_CURVE ( 'NONE', #99617, #137268, #117939, .T. ) ;
#115102=CARTESIAN_POINT ( 'NONE',  ( -19.82816939922338406, 9.759292476615620160, 4.000000000000000000 ) ) ;
#115103=ORIENTED_EDGE ( 'NONE', *, *, #27944, .F. ) ;
#115105=VECTOR ( 'NONE', #143087, 1000.000000000000000 ) ;
#115106=CARTESIAN_POINT ( 'NONE',  ( -57.18398860626899705, 28.73617430169827358, 5.000000000000000000 ) ) ;
#115107=EDGE_CURVE ( 'NONE', #12703, #816, #128847, .T. ) ;
#115110=LINE ( 'NONE', #96220, #86375 ) ;
#115111=DIRECTION ( 'NONE',  ( -0.000000000000000000, 0.3543493200069153248, 0.9351131265310292928 ) ) ;
#115112=EDGE_CURVE ( 'NONE', #63799, #5098, #62917, .T. ) ;
#115114=VERTEX_POINT ( 'NONE', #96200 ) ;
#115115=ORIENTED_EDGE ( 'NONE', *, *, #59669, .T. ) ;
#115116=VERTEX_POINT ( 'NONE', #41129 ) ;
#115118=CARTESIAN_POINT ( 'NONE',  ( 30.51665438641024153, 22.22500000000000142, 4.500000000000000888 ) ) ;
#115119=AXIS2_PLACEMENT_3D ( 'NONE', #38932, #137544, #83153 ) ;
#115120=CARTESIAN_POINT ( 'NONE',  ( -36.29974487139159578, -27.71228299555231445, 4.000000000000000000 ) ) ;
#115121=DIRECTION ( 'NONE',  ( -0.6830127018922181881, 0.6830127018922202975, -0.2588190451025214056 ) ) ;
#115122=LINE ( 'NONE', #26023, #129513 ) ;
#115123=CARTESIAN_POINT ( 'NONE',  ( 17.61782366839360847, 8.969638207445433054, 4.000000000000000000 ) ) ;
#115124=EDGE_CURVE ( 'NONE', #71084, #127668, #10622, .T. ) ;
#115125=DIRECTION ( 'NONE',  ( -0.000000000000000000, 0.000000000000000000, 1.000000000000000000 ) ) ;
#115127=PLANE ( 'NONE',  #76723 ) ;
#115128=ORIENTED_EDGE ( 'NONE', *, *, #117739, .F. ) ;
#115129=LINE ( 'NONE', #103557, #132039 ) ;
#115130=EDGE_CURVE ( 'NONE', #112685, #86810, #86796, .T. ) ;
#115132=ORIENTED_EDGE ( 'NONE', *, *, #6698, .T. ) ;
#115133=CARTESIAN_POINT ( 'NONE',  ( -3.183988606268992161, 28.73617430169789699, 5.000000000000000000 ) ) ;
#115135=VERTEX_POINT ( 'NONE', #133857 ) ;
#115136=ORIENTED_EDGE ( 'NONE', *, *, #46662, .F. ) ;
#115137=DIRECTION ( 'NONE',  ( -0.000000000000000000, -0.3543493200069152693, 0.9351131265310292928 ) ) ;
#115139=DIRECTION ( 'NONE',  ( -0.000000000000000000, 0.3543493200069153248, 0.9351131265310291818 ) ) ;
#115140=VECTOR ( 'NONE', #28680, 1000.000000000000000 ) ;
#115141=EDGE_CURVE ( 'NONE', #80852, #137944, #120080, .T. ) ;
#115142=EDGE_LOOP ( 'NONE', ( #111544, #5461, #112739, #72935 ) ) ;
#115143=ADVANCED_FACE ( 'NONE', ( #131720 ), #57043, .F. ) ;
#115145=DIRECTION ( 'NONE',  ( -0.7071067811865486830, -0.7071067811865464625, 0.000000000000000000 ) ) ;
#115148=DIRECTION ( 'NONE',  ( -0.7071067811865486830, 0.7071067811865464625, 0.000000000000000000 ) ) ;
#115149=DIRECTION ( 'NONE',  ( -0.7071067811865486830, 0.7071067811865464625, 0.000000000000000000 ) ) ;
#115150=CARTESIAN_POINT ( 'NONE',  ( -51.48921356237309510, -27.52281430457091460, 5.000000000000000000 ) ) ;
#115151=CARTESIAN_POINT ( 'NONE',  ( 2.292893218813443657, 2.259292476615692546, 5.000000000000000000 ) ) ;
#115156=DIRECTION ( 'NONE',  ( -0.7071067811865486830, -0.7071067811865464625, 0.000000000000000000 ) ) ;
#115157=LINE ( 'NONE', #123954, #62831 ) ;
#115159=ORIENTED_EDGE ( 'NONE', *, *, #21262, .F. ) ;
#115160=( BOUNDED_CURVE ( )  B_SPLINE_CURVE ( 3, ( #12818, #37465, #101993, #90398 ),
 .UNSPECIFIED., .F., .T. ) 
 B_SPLINE_CURVE_WITH_KNOTS ( ( 4, 4 ),
 ( 4.350170835173029715, 4.500739107949206286 ),
 .UNSPECIFIED. ) 
 CURVE ( )  GEOMETRIC_REPRESENTATION_ITEM ( )  RATIONAL_B_SPLINE_CURVE ( ( 1.000000000000000000, 0.9981116584018959736, 0.9981116584018959736, 1.000000000000000000 ) ) 
 REPRESENTATION_ITEM ( '' )  );
#115161=ADVANCED_FACE ( 'NONE', ( #143297 ), #112119, .F. ) ;
#115163=ADVANCED_FACE ( 'NONE', ( #121536 ), #34547, .F. ) ;
#115165=VERTEX_POINT ( 'NONE', #21529 ) ;
#115166=EDGE_LOOP ( 'NONE', ( #99774, #110376, #62609, #109963 ) ) ;
#115168=DIRECTION ( 'NONE',  ( -0.000000000000000000, 0.3543493200069153248, 0.9351131265310292928 ) ) ;
#115169=VERTEX_POINT ( 'NONE', #101214 ) ;
#115171=EDGE_CURVE ( 'NONE', #20015, #98883, #131014, .T. ) ;
#115173=LINE ( 'NONE', #137701, #27900 ) ;
#115175=ADVANCED_FACE ( 'NONE', ( #99055 ), #11316, .F. ) ;
#115176=FACE_OUTER_BOUND ( 'NONE', #79999, .T. ) ;
#115177=DIRECTION ( 'NONE',  ( 0.7071067811865486830, -0.7071067811865464625, -0.000000000000000000 ) ) ;
#115178=CARTESIAN_POINT ( 'NONE',  ( 30.29974487139158867, -27.71228299555227537, 4.000000000000000000 ) ) ;
#115179=DIRECTION ( 'NONE',  ( -0.000000000000000000, -0.3543493200069152693, 0.9351131265310292928 ) ) ;
#115180=LINE ( 'NONE', #128948, #77636 ) ;
#115181=CARTESIAN_POINT ( 'NONE',  ( 33.18398860626899705, 28.73617430169810305, 5.000000000000000000 ) ) ;
#115183=VERTEX_POINT ( 'NONE', #44000 ) ;
#115184=VERTEX_POINT ( 'NONE', #100525 ) ;
#115186=AXIS2_PLACEMENT_3D ( 'NONE', #116359, #104766, #39536 ) ;
#115187=ORIENTED_EDGE ( 'NONE', *, *, #32742, .T. ) ;
#115188=EDGE_CURVE ( 'NONE', #130548, #9302, #55598, .T. ) ;
#115189=LINE ( 'NONE', #125408, #126561 ) ;
#115190=VERTEX_POINT ( 'NONE', #31690 ) ;
#115191=EDGE_CURVE ( 'NONE', #111380, #108455, #75909, .T. ) ;
#115192=DIRECTION ( 'NONE',  ( 0.7071067811865487940, 0.7071067811865463515, -0.000000000000000000 ) ) ;
#115193=DIRECTION ( 'NONE',  ( -0.7071067811865486830, -0.7071067811865464625, 0.000000000000000000 ) ) ;
#115194=VECTOR ( 'NONE', #106075, 1000.000000000000000 ) ;
#115196=EDGE_LOOP ( 'NONE', ( #59998, #24387, #72569, #55129 ) ) ;
#115197=VERTEX_POINT ( 'NONE', #89631 ) ;
#115198=LINE ( 'NONE', #81210, #119439 ) ;
#115199=FACE_OUTER_BOUND ( 'NONE', #21200, .T. ) ;
#115200=DIRECTION ( 'NONE',  ( 0.3543493200069162685, -0.000000000000000000, -0.9351131265310288487 ) ) ;
#115201=AXIS2_PLACEMENT_3D ( 'NONE', #45459, #88956, #66482 ) ;
#115202=ORIENTED_EDGE ( 'NONE', *, *, #57438, .F. ) ;
#115203=ORIENTED_EDGE ( 'NONE', *, *, #25504, .F. ) ;
#115204=VECTOR ( 'NONE', #11280, 1000.000000000000227 ) ;
#115205=ORIENTED_EDGE ( 'NONE', *, *, #69339, .F. ) ;
#115206=CARTESIAN_POINT ( 'NONE',  ( -24.79593897580385331, 4.791522900035168675, 4.000000000000000000 ) ) ;
#115209=VECTOR ( 'NONE', #71802, 1000.000000000000227 ) ;
#115210=DIRECTION ( 'NONE',  ( 1.000000000000000000, 0.000000000000000000, 0.000000000000000000 ) ) ;
#115211=EDGE_CURVE ( 'NONE', #141554, #121112, #122241, .T. ) ;
#115215=CARTESIAN_POINT ( 'NONE',  ( -37.44665057663194574, 2.259292476615697876, 14.86850063742363126 ) ) ;
#115217=VERTEX_POINT ( 'NONE', #109241 ) ;
#115218=PLANE ( 'NONE',  #7715 ) ;
#115219=DIRECTION ( 'NONE',  ( -0.7071067811865486830, -0.7071067811865464625, 0.000000000000000000 ) ) ;
#115220=CARTESIAN_POINT ( 'NONE',  ( 63.18398860626900415, 28.73617430169831621, 5.000000000000000000 ) ) ;
#115221=ORIENTED_EDGE ( 'NONE', *, *, #13048, .F. ) ;
#115222=CARTESIAN_POINT ( 'NONE',  ( -7.828169399223476432, 21.75929247661548871, 4.000000000000000000 ) ) ;
#115223=PLANE ( 'NONE',  #38647 ) ;
#115224=LINE ( 'NONE', #47225, #64535 ) ;
#115225=LINE ( 'NONE', #15909, #113811 ) ;
#115226=DIRECTION ( 'NONE',  ( -0.7071067811865487940, 0.7071067811865463515, -0.000000000000000000 ) ) ;
#115227=FACE_BOUND ( 'NONE', #105299, .T. ) ;
#115229=CARTESIAN_POINT ( 'NONE',  ( 48.29974487139158867, -27.71228299555239971, 4.000000000000000000 ) ) ;
#115230=FACE_OUTER_BOUND ( 'NONE', #4345, .T. ) ;
#115231=LINE ( 'NONE', #39156, #88542 ) ;
#115232=ORIENTED_EDGE ( 'NONE', *, *, #7755, .F. ) ;
#115233=CARTESIAN_POINT ( 'NONE',  ( -25.49999999999982236, 12.05218569542904561, 5.000000000000000000 ) ) ;
#115234=ORIENTED_EDGE ( 'NONE', *, *, #3583, .T. ) ;
#115235=VECTOR ( 'NONE', #43611, 1000.000000000000000 ) ;
#115239=VERTEX_POINT ( 'NONE', #22911 ) ;
#115240=CARTESIAN_POINT ( 'NONE',  ( 57.48921356237308800, -27.52281430457095368, 5.000000000000000000 ) ) ;
#115241=PLANE ( 'NONE',  #108669 ) ;
#115242=CARTESIAN_POINT ( 'NONE',  ( 14.29320749275917635, 20.25929247661551358, 20.83292124670811418 ) ) ;
#115243=VERTEX_POINT ( 'NONE', #67177 ) ;
#115245=LINE ( 'NONE', #4314, #70078 ) ;
#115247=DIRECTION ( 'NONE',  ( 0.000000000000000000, -1.000000000000000000, 0.000000000000000000 ) ) ;
#115248=DIRECTION ( 'NONE',  ( 0.7071067811865487940, 0.7071067811865463515, 0.000000000000000000 ) ) ;
#115249=DIRECTION ( 'NONE',  ( -0.7071067811865486830, -0.7071067811865464625, -0.000000000000000000 ) ) ;
#115250=CARTESIAN_POINT ( 'NONE',  ( 32.99999999999975842, 14.58746187583910192, 4.000000000000000000 ) ) ;
#115253=ORIENTED_EDGE ( 'NONE', *, *, #121467, .F. ) ;
#115254=EDGE_LOOP ( 'NONE', ( #109068, #98864, #76854, #86731 ) ) ;
#115255=ORIENTED_EDGE ( 'NONE', *, *, #70389, .F. ) ;
#115257=ORIENTED_EDGE ( 'NONE', *, *, #61589, .T. ) ;
#115259=VERTEX_POINT ( 'NONE', #111368 ) ;
#115260=DIRECTION ( 'NONE',  ( 0.7071067811865487940, 0.7071067811865463515, 0.000000000000000000 ) ) ;
#115261=DIRECTION ( 'NONE',  ( 0.7071067811865487940, -0.7071067811865463515, 0.000000000000000000 ) ) ;
#115262=EDGE_CURVE ( 'NONE', #124292, #2262, #12059, .T. ) ;
#115263=EDGE_CURVE ( 'NONE', #33303, #80619, #112807, .T. ) ;
#115264=CARTESIAN_POINT ( 'NONE',  ( 26.99999999999981526, -6.108550654416935011, -3.114665004254905334 ) ) ;
#115265=ORIENTED_EDGE ( 'NONE', *, *, #52470, .T. ) ;
#115266=DIRECTION ( 'NONE',  ( 0.7071067811865487940, -0.7071067811865463515, 0.000000000000000000 ) ) ;
#115267=VERTEX_POINT ( 'NONE', #70073 ) ;
#115268=LINE ( 'NONE', #95700, #60618 ) ;
#115269=EDGE_CURVE ( 'NONE', #47748, #36255, #2601, .T. ) ;
#115270=ADVANCED_FACE ( 'NONE', ( #4702 ), #48999, .F. ) ;
#115271=LINE ( 'NONE', #37780, #63567 ) ;
#115273=ORIENTED_EDGE ( 'NONE', *, *, #40711, .T. ) ;
#115275=CARTESIAN_POINT ( 'NONE',  ( 1.499999999999987566, 12.05218569542904561, 5.000000000000000000 ) ) ;
#115278=DIRECTION ( 'NONE',  ( -0.7071067811865486830, -0.7071067811865464625, -0.000000000000000000 ) ) ;
#115279=CARTESIAN_POINT ( 'NONE',  ( -29.99999999999979039, 12.25461709320618553, -10.07315571508704188 ) ) ;
#115281=EDGE_LOOP ( 'NONE', ( #117372, #117204, #112130, #80110 ) ) ;
#115282=DIRECTION ( 'NONE',  ( -0.000000000000000000, -0.3543493200069152693, 0.9351131265310292928 ) ) ;
#115283=ORIENTED_EDGE ( 'NONE', *, *, #15473, .T. ) ;
#115284=FACE_OUTER_BOUND ( 'NONE', #123767, .T. ) ;
#115285=DIRECTION ( 'NONE',  ( 0.6830127018922180770, -0.6830127018922204085, -0.2588190451025213501 ) ) ;
#115286=DIRECTION ( 'NONE',  ( 0.000000000000000000, 0.000000000000000000, -1.000000000000000000 ) ) ;
#115288=EDGE_LOOP ( 'NONE', ( #77745, #58405, #62380, #85798 ) ) ;
#115289=DIRECTION ( 'NONE',  ( 0.000000000000000000, 1.000000000000000000, -0.000000000000000000 ) ) ;
#115290=EDGE_CURVE ( 'NONE', #51730, #16952, #48265, .T. ) ;
#115291=PLANE ( 'NONE',  #81212 ) ;
#115292=DIRECTION ( 'NONE',  ( -0.000000000000000000, -0.3543493200069152693, 0.9351131265310292928 ) ) ;
#115293=EDGE_LOOP ( 'NONE', ( #25563, #61304, #3739, #14891 ) ) ;
#115294=FACE_OUTER_BOUND ( 'NONE', #113530, .T. ) ;
#115295=CARTESIAN_POINT ( 'NONE',  ( -13.78678096696632061, 12.75929247661558996, 10.29404684609032117 ) ) ;
#115299=ORIENTED_EDGE ( 'NONE', *, *, #100267, .T. ) ;
#115300=EDGE_LOOP ( 'NONE', ( #52729, #112398, #38771, #19367 ) ) ;
#115303=EDGE_CURVE ( 'NONE', #97211, #52188, #101938, .T. ) ;
#115304=AXIS2_PLACEMENT_3D ( 'NONE', #49541, #50944, #138672 ) ;
#115305=VERTEX_POINT ( 'NONE', #81645 ) ;
#115306=PLANE ( 'NONE',  #14113 ) ;
#115307=AXIS2_PLACEMENT_3D ( 'NONE', #104202, #69494, #113678 ) ;
#115308=LINE ( 'NONE', #39975, #77506 ) ;
#115310=( BOUNDED_CURVE ( )  B_SPLINE_CURVE ( 3, ( #74206, #82247, #116274, #27113 ),
 .UNSPECIFIED., .F., .T. ) 
 B_SPLINE_CURVE_WITH_KNOTS ( ( 4, 4 ),
 ( 2.779374508378135378, 4.199602562396837158 ),
 .UNSPECIFIED. ) 
 CURVE ( )  GEOMETRIC_REPRESENTATION_ITEM ( )  RATIONAL_B_SPLINE_CURVE ( ( 1.000000000000000000, 0.8388583629366632710, 0.8388583629366632710, 1.000000000000000000 ) ) 
 REPRESENTATION_ITEM ( '' )  );
#115311=ORIENTED_EDGE ( 'NONE', *, *, #65018, .F. ) ;
#115312=CARTESIAN_POINT ( 'NONE',  ( -18.32816939922339827, -21.74070752338405654, 4.000000000000000000 ) ) ;
#115313=CARTESIAN_POINT ( 'NONE',  ( -39.18398860626899705, 28.73617430169814568, 5.000000000000000000 ) ) ;
#115314=CARTESIAN_POINT ( 'NONE',  ( -30.29974487139158867, -27.71228299555227537, 4.000000000000000000 ) ) ;
#115315=CARTESIAN_POINT ( 'NONE',  ( -5.994519915287488843, 28.92564299267942118, 4.000000000000000000 ) ) ;
#115320=CARTESIAN_POINT ( 'NONE',  ( -27.29974487139158512, -27.71228299555225405, 4.000000000000000000 ) ) ;
#115322=EDGE_LOOP ( 'NONE', ( #83891, #117606, #15896, #134935 ) ) ;
#115323=ORIENTED_EDGE ( 'NONE', *, *, #104175, .F. ) ;
#115324=ORIENTED_EDGE ( 'NONE', *, *, #110757, .T. ) ;
#115325=ADVANCED_FACE ( 'NONE', ( #82347 ), #125110, .F. ) ;
#115327=EDGE_LOOP ( 'NONE', ( #84545, #193, #110553, #51606 ) ) ;
#115329=ADVANCED_FACE ( 'NONE', ( #103340 ), #3989, .F. ) ;
#115331=CARTESIAN_POINT ( 'NONE',  ( -12.32816939922344979, -3.740707523384244837, 4.000000000000000000 ) ) ;
#115332=VECTOR ( 'NONE', #55494, 1000.000000000000000 ) ;
#115333=DIRECTION ( 'NONE',  ( 0.6830127018922181881, 0.6830127018922202975, -0.2588190451025214056 ) ) ;
#115334=VERTEX_POINT ( 'NONE', #90343 ) ;
#115335=PLANE ( 'NONE',  #117919 ) ;
#115336=AXIS2_PLACEMENT_3D ( 'NONE', #101793, #46015, #70642 ) ;
#115337=ADVANCED_FACE ( 'NONE', ( #126529 ), #79531, .F. ) ;
#115339=LINE ( 'NONE', #117498, #72100 ) ;
#115341=EDGE_LOOP ( 'NONE', ( #82296, #18250, #113720, #92813 ) ) ;
#115343=FACE_OUTER_BOUND ( 'NONE', #8384, .T. ) ;
#115344=LINE ( 'NONE', #36408, #52011 ) ;
#115346=CARTESIAN_POINT ( 'NONE',  ( -20.99451991528748707, 28.92564299267952777, 4.000000000000000000 ) ) ;
#115347=( BOUNDED_CURVE ( )  B_SPLINE_CURVE ( 3, ( #100389, #35872, #56906, #1727 ),
 .UNSPECIFIED., .F., .F. ) 
 B_SPLINE_CURVE_WITH_KNOTS ( ( 4, 4 ),
 ( 0.8834430019029047010, 0.8929338002999916979 ),
 .UNSPECIFIED. ) 
 CURVE ( )  GEOMETRIC_REPRESENTATION_ITEM ( )  RATIONAL_B_SPLINE_CURVE ( ( 1.000000000000000000, 0.9999924937429014449, 0.9999924937429014449, 1.000000000000000000 ) ) 
 REPRESENTATION_ITEM ( '' )  );
#115348=ADVANCED_FACE ( 'NONE', ( #25796 ), #104788, .T. ) ;
#115349=CARTESIAN_POINT ( 'NONE',  ( 17.48334561358943162, 22.22500000000000142, 4.500000000000000888 ) ) ;
#115350=FACE_OUTER_BOUND ( 'NONE', #113192, .T. ) ;
#115353=DIRECTION ( 'NONE',  ( -0.6830127018922180770, -0.6830127018922204085, -0.2588190451025213501 ) ) ;
#115354=ORIENTED_EDGE ( 'NONE', *, *, #141056, .T. ) ;
#115355=VERTEX_POINT ( 'NONE', #116383 ) ;
#115358=ORIENTED_EDGE ( 'NONE', *, *, #6976, .F. ) ;
#115359=EDGE_CURVE ( 'NONE', #52699, #44719, #49731, .T. ) ;
#115360=DIRECTION ( 'NONE',  ( -0.7071067811865486830, 0.7071067811865463515, 0.000000000000000000 ) ) ;
#115361=DIRECTION ( 'NONE',  ( -0.6830127018922180770, -0.6830127018922204085, -0.2588190451025213501 ) ) ;
#115363=VECTOR ( 'NONE', #57930, 1000.000000000000000 ) ;
#115364=CARTESIAN_POINT ( 'NONE',  ( -34.92500000000001137, -22.22500000000000142, 4.000000000000000000 ) ) ;
#115365=DIRECTION ( 'NONE',  ( -0.7071067811865487940, 0.7071067811865463515, 0.000000000000000000 ) ) ;
#115367=DIRECTION ( 'NONE',  ( -0.7071067811865487940, 0.7071067811865463515, 0.000000000000000000 ) ) ;
#115369=ORIENTED_EDGE ( 'NONE', *, *, #85716, .T. ) ;
#115370=DIRECTION ( 'NONE',  ( -0.6830127018922180770, -0.6830127018922204085, -0.2588190451025213501 ) ) ;
#115372=LINE ( 'NONE', #50880, #138792 ) ;
#115373=DIRECTION ( 'NONE',  ( 0.7071067811865486830, -0.7071067811865464625, -0.000000000000000000 ) ) ;
#115376=ORIENTED_EDGE ( 'NONE', *, *, #135957, .T. ) ;
#115377=ADVANCED_FACE ( 'NONE', ( #62740 ), #28682, .T. ) ;
#115378=VERTEX_POINT ( 'NONE', #85167 ) ;
#115379=LINE ( 'NONE', #50893, #142048 ) ;
#115380=DIRECTION ( 'NONE',  ( 0.7071067811865487940, -0.7071067811865463515, 0.000000000000000000 ) ) ;
#115382=ADVANCED_FACE ( 'NONE', ( #119222 ), #7598, .F. ) ;
#115384=ORIENTED_EDGE ( 'NONE', *, *, #143042, .F. ) ;
#115385=CARTESIAN_POINT ( 'NONE',  ( 0.000000000000000000, 0.000000000000000000, 5.000000000000000000 ) ) ;
#115386=CARTESIAN_POINT ( 'NONE',  ( -11.99999999999992006, 10.93112307739207267, 4.000000000000000000 ) ) ;
#115389=CARTESIAN_POINT ( 'NONE',  ( 30.32816939922331656, -0.7407075233842805861, 4.000000000000000000 ) ) ;
#115390=ORIENTED_EDGE ( 'NONE', *, *, #47549, .F. ) ;
#115391=EDGE_CURVE ( 'NONE', #85257, #125144, #95334, .T. ) ;
#115392=EDGE_CURVE ( 'NONE', #9454, #16274, #130127, .T. ) ;
#115393=VECTOR ( 'NONE', #5107, 999.9999999999998863 ) ;
#115394=CARTESIAN_POINT ( 'NONE',  ( 21.18398860626899349, 28.73617430169802134, 5.000000000000000000 ) ) ;
#115395=ORIENTED_EDGE ( 'NONE', *, *, #115986, .F. ) ;
#115396=DIRECTION ( 'NONE',  ( -0.000000000000000000, 0.3543493200069153248, 0.9351131265310292928 ) ) ;
#115397=LINE ( 'NONE', #16088, #47889 ) ;
#115399=VECTOR ( 'NONE', #77396, 1000.000000000000000 ) ;
#115400=VECTOR ( 'NONE', #90687, 1000.000000000000227 ) ;
#115401=DIRECTION ( 'NONE',  ( 1.000000000000000000, 0.000000000000000000, 0.000000000000000000 ) ) ;
#115403=FACE_BOUND ( 'NONE', #118866, .T. ) ;
#115404=EDGE_CURVE ( 'NONE', #42067, #121003, #105485, .T. ) ;
#115405=LINE ( 'NONE', #124900, #112833 ) ;
#115406=DIRECTION ( 'NONE',  ( 0.3543493200069162685, -0.000000000000000000, -0.9351131265310288487 ) ) ;
#115407=FACE_OUTER_BOUND ( 'NONE', #22393, .T. ) ;
#115408=EDGE_LOOP ( 'NONE', ( #60921, #80246, #102428, #102159 ) ) ;
#115409=CARTESIAN_POINT ( 'NONE',  ( 18.48921356237309510, -27.52281430457068367, 5.000000000000000000 ) ) ;
#115411=VERTEX_POINT ( 'NONE', #72926 ) ;
#115412=VECTOR ( 'NONE', #115249, 1000.000000000000000 ) ;
#115413=VECTOR ( 'NONE', #140155, 999.9999999999998863 ) ;
#115415=VERTEX_POINT ( 'NONE', #106920 ) ;
#115416=VERTEX_POINT ( 'NONE', #93907 ) ;
#115418=ORIENTED_EDGE ( 'NONE', *, *, #110427, .F. ) ;
#115419=DIRECTION ( 'NONE',  ( -0.7071067811865486830, 0.7071067811865464625, 0.000000000000000000 ) ) ;
#115420=DIRECTION ( 'NONE',  ( 0.3543493200069162685, -0.000000000000000000, -0.9351131265310288487 ) ) ;
#115421=ORIENTED_EDGE ( 'NONE', *, *, #62820, .F. ) ;
#115422=CARTESIAN_POINT ( 'NONE',  ( -34.92500000000001137, 19.51246187583930336, 4.000000000000000000 ) ) ;
#115423=AXIS2_PLACEMENT_3D ( 'NONE', #104278, #26041, #48497 ) ;
#115424=CIRCLE ( 'NONE', #50699, 3.378199999999997871 ) ;
#115425=DIRECTION ( 'NONE',  ( -0.6830127018922181881, 0.6830127018922202975, -0.2588190451025214056 ) ) ;
#115427=PLANE ( 'NONE',  #131510 ) ;
#115428=DIRECTION ( 'NONE',  ( -0.000000000000000000, 0.3543493200069153248, 0.9351131265310292928 ) ) ;
#115429=PLANE ( 'NONE',  #78717 ) ;
#115430=ORIENTED_EDGE ( 'NONE', *, *, #61365, .F. ) ;
#115431=AXIS2_PLACEMENT_3D ( 'NONE', #45157, #135013, #866 ) ;
#115432=ORIENTED_EDGE ( 'NONE', *, *, #69537, .F. ) ;
#115433=DIRECTION ( 'NONE',  ( 0.6830127018922180770, -0.6830127018922204085, -0.2588190451025213501 ) ) ;
#115435=ORIENTED_EDGE ( 'NONE', *, *, #139142, .F. ) ;
#115436=VECTOR ( 'NONE', #54930, 1000.000000000000000 ) ;
#115437=EDGE_LOOP ( 'NONE', ( #41197, #20688, #106403, #12736 ) ) ;
#115439=ORIENTED_EDGE ( 'NONE', *, *, #48082, .F. ) ;
#115440=FACE_OUTER_BOUND ( 'NONE', #86882, .T. ) ;
#115441=EDGE_CURVE ( 'NONE', #37944, #55809, #18458, .T. ) ;
#115442=DIRECTION ( 'NONE',  ( -0.000000000000000000, -0.000000000000000000, 1.000000000000000000 ) ) ;
#115443=ORIENTED_EDGE ( 'NONE', *, *, #72717, .T. ) ;
#115444=AXIS2_PLACEMENT_3D ( 'NONE', #17302, #61564, #105713 ) ;
#115445=DIRECTION ( 'NONE',  ( -0.000000000000000000, 0.3543493200069153248, 0.9351131265310292928 ) ) ;
#115447=ADVANCED_FACE ( 'NONE', ( #117076 ), #140282, .F. ) ;
#115448=EDGE_CURVE ( 'NONE', #137834, #96838, #107636, .T. ) ;
#115450=CARTESIAN_POINT ( 'NONE',  ( 9.299744871391588674, -27.71228299555212971, 4.000000000000000000 ) ) ;
#115451=EDGE_CURVE ( 'NONE', #3406, #89682, #94610, .T. ) ;
#115452=VERTEX_POINT ( 'NONE', #17753 ) ;
#115453=PLANE ( 'NONE',  #43468 ) ;
#115454=ADVANCED_FACE ( 'NONE', ( #40970 ), #38829, .F. ) ;
#115455=LINE ( 'NONE', #105327, #141526 ) ;
#115456=CARTESIAN_POINT ( 'NONE',  ( -23.99451991528749062, 28.92564299267954908, 4.000000000000000000 ) ) ;
#115458=CARTESIAN_POINT ( 'NONE',  ( -16.82816939922340893, -14.24070752338413826, 4.000000000000000000 ) ) ;
#115459=ORIENTED_EDGE ( 'NONE', *, *, #36877, .F. ) ;
#115460=ORIENTED_EDGE ( 'NONE', *, *, #62620, .T. ) ;
#115461=EDGE_CURVE ( 'NONE', #56410, #19080, #8460, .T. ) ;
#115463=DIRECTION ( 'NONE',  ( 0.7071067811865486830, -0.7071067811865464625, -0.000000000000000000 ) ) ;
#115464=CARTESIAN_POINT ( 'NONE',  ( -9.707106781186478628, 14.25929247661557753, 5.000000000000000000 ) ) ;
#115465=VERTEX_POINT ( 'NONE', #62028 ) ;
#115466=EDGE_CURVE ( 'NONE', #66246, #44911, #127999, .T. ) ;
#115467=CARTESIAN_POINT ( 'NONE',  ( 27.27825451568556048, 8.259292476615630818, 11.78515199841156935 ) ) ;
#115468=FACE_OUTER_BOUND ( 'NONE', #125099, .T. ) ;
#115469=PLANE ( 'NONE',  #76834 ) ;
#115470=ORIENTED_EDGE ( 'NONE', *, *, #68395, .F. ) ;
#115471=DIRECTION ( 'NONE',  ( 0.7071067811865486830, -0.7071067811865464625, -0.000000000000000000 ) ) ;
#115472=DIRECTION ( 'NONE',  ( -0.000000000000000000, 0.3543493200069153248, 0.9351131265310292928 ) ) ;
#115474=EDGE_CURVE ( 'NONE', #7430, #115805, #139601, .T. ) ;
#115475=LINE ( 'NONE', #116940, #63453 ) ;
#115476=CARTESIAN_POINT ( 'NONE',  ( 29.14818355038126896, 17.25929247661554200, 8.802941693769270159 ) ) ;
#115477=ORIENTED_EDGE ( 'NONE', *, *, #92811, .F. ) ;
#115478=ORIENTED_EDGE ( 'NONE', *, *, #124511, .T. ) ;
#115479=PLANE ( 'NONE',  #130604 ) ;
#115480=CARTESIAN_POINT ( 'NONE',  ( 5.292893218813423672, -18.74070752338408852, 5.000000000000000000 ) ) ;
#115484=CARTESIAN_POINT ( 'NONE',  ( -15.18398860626900237, 28.73617430169797871, 5.000000000000000000 ) ) ;
#115485=LINE ( 'NONE', #19067, #18142 ) ;
#115487=ORIENTED_EDGE ( 'NONE', *, *, #4892, .F. ) ;
#115488=CARTESIAN_POINT ( 'NONE',  ( -4.591674519009967703, -0.7407075233842735917, 14.76736230305379571 ) ) ;
#115489=CARTESIAN_POINT ( 'NONE',  ( 26.99999999999980815, -2.904428200921286951, -6.989807076075007508 ) ) ;
#115490=FACE_OUTER_BOUND ( 'NONE', #21093, .T. ) ;
#115492=CARTESIAN_POINT ( 'NONE',  ( -54.18398860626899705, 28.73617430169825226, 5.000000000000000000 ) ) ;
#115494=VERTEX_POINT ( 'NONE', #55421 ) ;
#115496=ORIENTED_EDGE ( 'NONE', *, *, #128450, .F. ) ;
#115498=CARTESIAN_POINT ( 'NONE',  ( 2.700255128608413990, -27.71228299555204089, 4.000000000000000000 ) ) ;
#115500=AXIS2_PLACEMENT_3D ( 'NONE', #23994, #124726, #100132 ) ;
#115501=AXIS2_PLACEMENT_3D ( 'NONE', #46088, #24305, #80147 ) ;
#115502=EDGE_CURVE ( 'NONE', #27206, #141564, #67006, .T. ) ;
#115504=DIRECTION ( 'NONE',  ( -0.7071067811865486830, -0.7071067811865464625, 0.000000000000000000 ) ) ;
#115506=CARTESIAN_POINT ( 'NONE',  ( 24.18398860626899705, 28.73617430169804265, 5.000000000000000000 ) ) ;
#115507=CARTESIAN_POINT ( 'NONE',  ( 51.29974487139158867, -27.71228299555242103, 4.000000000000000000 ) ) ;
#115509=EDGE_LOOP ( 'NONE', ( #25239, #103012, #11368 ) ) ;
#115510=LINE ( 'NONE', #126420, #30194 ) ;
#115511=DIRECTION ( 'NONE',  ( 0.7071067811865486830, -0.7071067811865464625, -0.000000000000000000 ) ) ;
#115513=VECTOR ( 'NONE', #66008, 1000.000000000000114 ) ;
#115514=LINE ( 'NONE', #51750, #111005 ) ;
#115515=LINE ( 'NONE', #37294, #70582 ) ;
#115516=ADVANCED_FACE ( 'NONE', ( #88774 ), #89459, .F. ) ;
#115517=DIRECTION ( 'NONE',  ( 0.7071067811865487940, -0.7071067811865463515, 0.000000000000000000 ) ) ;
#115519=FACE_OUTER_BOUND ( 'NONE', #133791, .T. ) ;
#115521=VERTEX_POINT ( 'NONE', #66304 ) ;
#115523=CARTESIAN_POINT ( 'NONE',  ( -19.49999999999986855, 22.01701374228154151, 2.453858888625676471 ) ) ;
#115524=EDGE_CURVE ( 'NONE', #100863, #53824, #64156, .T. ) ;
#115525=DIRECTION ( 'NONE',  ( 1.000000000000000000, 0.000000000000000000, 0.000000000000000000 ) ) ;
#115526=CARTESIAN_POINT ( 'NONE',  ( -3.005480084712505828, 28.92564299267936079, 4.000000000000000000 ) ) ;
#115527=VECTOR ( 'NONE', #136933, 1000.000000000000227 ) ;
#115528=VECTOR ( 'NONE', #111209, 1000.000000000000000 ) ;
#115529=ORIENTED_EDGE ( 'NONE', *, *, #47900, .F. ) ;
#115531=VECTOR ( 'NONE', #102409, 1000.000000000000227 ) ;
#115532=EDGE_CURVE ( 'NONE', #142336, #133793, #22738, .T. ) ;
#115533=CARTESIAN_POINT ( 'NONE',  ( 0.7070132642930391231, -21.74070752338405654, 4.999753212805213565 ) ) ;
#115535=LINE ( 'NONE', #14832, #36693 ) ;
#115536=VERTEX_POINT ( 'NONE', #11880 ) ;
#115537=ORIENTED_EDGE ( 'NONE', *, *, #107223, .T. ) ;
#115538=LINE ( 'NONE', #16230, #97881 ) ;
#115539=AXIS2_PLACEMENT_3D ( 'NONE', #103273, #3923, #77985 ) ;
#115540=VECTOR ( 'NONE', #143183, 1000.000000000000000 ) ;
#115541=PLANE ( 'NONE',  #22206 ) ;
#115542=VECTOR ( 'NONE', #141391, 1000.000000000000000 ) ;
#115544=EDGE_CURVE ( 'NONE', #37768, #92198, #8988, .T. ) ;
#115545=DIRECTION ( 'NONE',  ( -0.3543493200069162685, -0.000000000000000000, -0.9351131265310288487 ) ) ;
#115546=DIRECTION ( 'NONE',  ( -0.7071067811865486830, 0.7071067811865464625, 0.000000000000000000 ) ) ;
#115547=ORIENTED_EDGE ( 'NONE', *, *, #141793, .T. ) ;
#115548=LINE ( 'NONE', #138065, #131736 ) ;
#115550=CARTESIAN_POINT ( 'NONE',  ( 39.18398860626899705, 28.73617430169814568, 5.000000000000000000 ) ) ;
#115551=AXIS2_PLACEMENT_3D ( 'NONE', #57820, #101290, #113583 ) ;
#115552=LINE ( 'NONE', #106847, #138743 ) ;
#115554=ORIENTED_EDGE ( 'NONE', *, *, #5362, .T. ) ;
#115555=ORIENTED_EDGE ( 'NONE', *, *, #79753, .F. ) ;
#115556=DIRECTION ( 'NONE',  ( -0.000000000000000000, 0.000000000000000000, 1.000000000000000000 ) ) ;
#115557=LINE ( 'NONE', #48937, #132117 ) ;
#115558=LINE ( 'NONE', #114171, #70992 ) ;
#115559=DIRECTION ( 'NONE',  ( 1.000000000000000000, 0.000000000000000000, 0.000000000000000000 ) ) ;
#115560=ORIENTED_EDGE ( 'NONE', *, *, #61538, .T. ) ;
#115561=ORIENTED_EDGE ( 'NONE', *, *, #93272, .F. ) ;
#115562=DIRECTION ( 'NONE',  ( -0.6830127018922180770, -0.6830127018922204085, -0.2588190451025213501 ) ) ;
#115566=EDGE_CURVE ( 'NONE', #138000, #141315, #133003, .T. ) ;
#115567=DIRECTION ( 'NONE',  ( -0.7071067811865486830, -0.7071067811865464625, 0.000000000000000000 ) ) ;
#115569=DIRECTION ( 'NONE',  ( -1.000000000000000000, 0.000000000000000000, -0.000000000000000000 ) ) ;
#115570=CARTESIAN_POINT ( 'NONE',  ( 0.000000000000000000, 0.000000000000000000, 5.000000000000000000 ) ) ;
#115571=FACE_BOUND ( 'NONE', #61351, .T. ) ;
#115572=EDGE_CURVE ( 'NONE', #102891, #73062, #10455, .T. ) ;
#115573=CARTESIAN_POINT ( 'NONE',  ( -62.99451991528749772, 28.92564299267982264, 4.000000000000000000 ) ) ;
#115574=PLANE ( 'NONE',  #4966 ) ;
#115575=DIRECTION ( 'NONE',  ( 1.000000000000000000, 0.000000000000000000, 0.000000000000000000 ) ) ;
#115579=ORIENTED_EDGE ( 'NONE', *, *, #42361, .T. ) ;
#115580=ORIENTED_EDGE ( 'NONE', *, *, #130264, .F. ) ;
#115582=EDGE_LOOP ( 'NONE', ( #94102, #2111, #62172, #35982 ) ) ;
#115583=CARTESIAN_POINT ( 'NONE',  ( 0.000000000000000000, 0.000000000000000000, 5.000000000000000000 ) ) ;
#115584=LINE ( 'NONE', #37372, #125429 ) ;
#115586=ORIENTED_EDGE ( 'NONE', *, *, #87824, .T. ) ;
#115587=CARTESIAN_POINT ( 'NONE',  ( 24.29974487139158867, -27.71228299555223273, 4.000000000000000000 ) ) ;
#115588=LINE ( 'NONE', #128663, #43115 ) ;
#115589=DIRECTION ( 'NONE',  ( 0.6830127018922180770, -0.6830127018922204085, -0.2588190451025213501 ) ) ;
#115590=DIRECTION ( 'NONE',  ( -0.000000000000000000, -0.000000000000000000, 1.000000000000000000 ) ) ;
#115591=FACE_OUTER_BOUND ( 'NONE', #79131, .T. ) ;
#115593=CARTESIAN_POINT ( 'NONE',  ( -6.792893218813407685, -8.240707523384200428, 5.000000000000000000 ) ) ;
#115597=DIRECTION ( 'NONE',  ( 0.7071067811865486830, -0.7071067811865464625, -0.000000000000000000 ) ) ;
#115598=VECTOR ( 'NONE', #24143, 1000.000000000000000 ) ;
#115599=VERTEX_POINT ( 'NONE', #76470 ) ;
#115600=CARTESIAN_POINT ( 'NONE',  ( 17.99451991528748351, 28.92564299267950645, 4.000000000000000000 ) ) ;
#115601=( BOUNDED_CURVE ( )  B_SPLINE_CURVE ( 3, ( #113762, #45688, #34792, #112347 ),
 .UNSPECIFIED., .F., .T. ) 
 B_SPLINE_CURVE_WITH_KNOTS ( ( 4, 4 ),
 ( 5.920967161967928050, 7.341195215986584088 ),
 .UNSPECIFIED. ) 
 CURVE ( )  GEOMETRIC_REPRESENTATION_ITEM ( )  RATIONAL_B_SPLINE_CURVE ( ( 1.000000000000000000, 0.8388583629366732630, 0.8388583629366732630, 1.000000000000000000 ) ) 
 REPRESENTATION_ITEM ( '' )  );
#115602=CARTESIAN_POINT ( 'NONE',  ( -17.99999999999986855, 17.96639925780207747, 5.000000000000000000 ) ) ;
#115603=ADVANCED_FACE ( 'NONE', ( #98209 ), #21355, .F. ) ;
#115605=VERTEX_POINT ( 'NONE', #97465 ) ;
#115606=ORIENTED_EDGE ( 'NONE', *, *, #11458, .F. ) ;
#115607=ORIENTED_EDGE ( 'NONE', *, *, #88700, .T. ) ;
#115609=ORIENTED_EDGE ( 'NONE', *, *, #49910, .T. ) ;
#115612=AXIS2_PLACEMENT_3D ( 'NONE', #7441, #129230, #37978 ) ;
#115615=EDGE_CURVE ( 'NONE', #41257, #119805, #88041, .T. ) ;
#115618=DIRECTION ( 'NONE',  ( 0.3543493200069162685, -0.000000000000000000, -0.9351131265310288487 ) ) ;
#115619=EDGE_CURVE ( 'NONE', #58958, #124820, #68659, .T. ) ;
#115620=VERTEX_POINT ( 'NONE', #137263 ) ;
#115622=VECTOR ( 'NONE', #118766, 1000.000000000000000 ) ;
#115623=CARTESIAN_POINT ( 'NONE',  ( 34.75611968250419892, -3.187065745292582797, 4.955485411084882053 ) ) ;
#115624=CARTESIAN_POINT ( 'NONE',  ( 28.99806943317882002, -22.22500000000000142, 4.500000000000000888 ) ) ;
#115625=ORIENTED_EDGE ( 'NONE', *, *, #106814, .F. ) ;
#115626=ORIENTED_EDGE ( 'NONE', *, *, #6500, .T. ) ;
#115627=EDGE_CURVE ( 'NONE', #114036, #103815, #4521, .T. ) ;
#115628=CARTESIAN_POINT ( 'NONE',  ( 27.32816939922334853, 14.25929247661557397, 4.000000000000000000 ) ) ;
#115630=VERTEX_POINT ( 'NONE', #56881 ) ;
#115631=VECTOR ( 'NONE', #70852, 999.9999999999998863 ) ;
#115632=DIRECTION ( 'NONE',  ( -0.000000000000000000, -0.3543493200069152693, 0.9351131265310292928 ) ) ;
#115633=ORIENTED_EDGE ( 'NONE', *, *, #86765, .F. ) ;
#115634=EDGE_LOOP ( 'NONE', ( #56553, #142093, #91399, #93059 ) ) ;
#115635=ORIENTED_EDGE ( 'NONE', *, *, #114902, .T. ) ;
#115636=EDGE_CURVE ( 'NONE', #110801, #141891, #37224, .T. ) ;
#115637=VERTEX_POINT ( 'NONE', #48832 ) ;
#115638=LINE ( 'NONE', #94623, #68059 ) ;
#115639=VECTOR ( 'NONE', #5210, 1000.000000000000000 ) ;
#115640=VECTOR ( 'NONE', #77075, 1000.000000000000000 ) ;
#115641=FACE_OUTER_BOUND ( 'NONE', #136427, .T. ) ;
#115642=AXIS2_PLACEMENT_3D ( 'NONE', #126084, #7837, #94135 ) ;
#115643=EDGE_CURVE ( 'NONE', #17453, #73565, #125677, .T. ) ;
#115645=CARTESIAN_POINT ( 'NONE',  ( 26.67183060077627488, -9.740707523384191546, 4.000000000000000000 ) ) ;
#115646=ADVANCED_FACE ( 'NONE', ( #37959 ), #67755, .F. ) ;
#115647=AXIS2_PLACEMENT_3D ( 'NONE', #44367, #133496, #34183 ) ;
#115649=ORIENTED_EDGE ( 'NONE', *, *, #79867, .F. ) ;
#115650=AXIS2_PLACEMENT_3D ( 'NONE', #93108, #106083, #115525 ) ;
#115651=DIRECTION ( 'NONE',  ( 0.7071067811865487940, 0.7071067811865463515, -0.000000000000000000 ) ) ;
#115654=DIRECTION ( 'NONE',  ( -0.7071067811865486830, -0.7071067811865464625, -0.000000000000000000 ) ) ;
#115655=CARTESIAN_POINT ( 'NONE',  ( -5.277185695429377432, -21.72500000000000853, 5.000000000000000000 ) ) ;
#115656=VERTEX_POINT ( 'NONE', #102504 ) ;
#115658=ORIENTED_EDGE ( 'NONE', *, *, #116569, .F. ) ;
#115659=DIRECTION ( 'NONE',  ( -0.6830127018922180770, -0.6830127018922204085, -0.2588190451025213501 ) ) ;
#115660=LINE ( 'NONE', #80949, #18652 ) ;
#115661=EDGE_CURVE ( 'NONE', #57451, #31683, #24219, .T. ) ;
#115662=CARTESIAN_POINT ( 'NONE',  ( -14.48334561358944761, 22.22500000000000142, 4.500000000000000888 ) ) ;
#115663=DIRECTION ( 'NONE',  ( 0.6830127018922181881, 0.6830127018922202975, -0.2588190451025214056 ) ) ;
#115664=DIRECTION ( 'NONE',  ( -0.6830127018922181881, 0.6830127018922202975, -0.2588190451025214056 ) ) ;
#115667=CARTESIAN_POINT ( 'NONE',  ( 74.99451991528749772, 28.92564299267990435, 4.000000000000000000 ) ) ;
#115668=LINE ( 'NONE', #5499, #41464 ) ;
#115669=CARTESIAN_POINT ( 'NONE',  ( 72.18398860626899705, 28.73617430169837661, 5.000000000000000000 ) ) ;
#115670=DIRECTION ( 'NONE',  ( 1.000000000000000000, 0.000000000000000000, 0.000000000000000000 ) ) ;
#115671=EDGE_CURVE ( 'NONE', #91273, #30305, #25622, .T. ) ;
#115672=ORIENTED_EDGE ( 'NONE', *, *, #137421, .T. ) ;
#115674=CARTESIAN_POINT ( 'NONE',  ( -10.17183060077640810, -17.24070752338411694, 4.000000000000000000 ) ) ;
#115675=VERTEX_POINT ( 'NONE', #26357 ) ;
#115676=LINE ( 'NONE', #60678, #69145 ) ;
#115677=DIRECTION ( 'NONE',  ( -0.7071067811865486830, -0.7071067811865464625, 0.000000000000000000 ) ) ;
#115678=VERTEX_POINT ( 'NONE', #90915 ) ;
#115679=LINE ( 'NONE', #114965, #136621 ) ;
#115680=DIRECTION ( 'NONE',  ( 0.7071067811865486830, -0.7071067811865464625, -0.000000000000000000 ) ) ;
#115683=ORIENTED_EDGE ( 'NONE', *, *, #101611, .T. ) ;
#115684=DIRECTION ( 'NONE',  ( -0.7071067811865486830, -0.7071067811865464625, -0.000000000000000000 ) ) ;
#115686=CARTESIAN_POINT ( 'NONE',  ( 31.49999999999978684, 18.43112307739199451, 4.000000000000000000 ) ) ;
#115687=EDGE_CURVE ( 'NONE', #51279, #65170, #114066, .T. ) ;
#115690=DIRECTION ( 'NONE',  ( 0.7071067811865486830, -0.7071067811865464625, -0.000000000000000000 ) ) ;
#115691=ORIENTED_EDGE ( 'NONE', *, *, #10811, .F. ) ;
#115692=CARTESIAN_POINT ( 'NONE',  ( -57.29974487139158157, -27.71228299555246011, 4.000000000000000000 ) ) ;
#115693=ADVANCED_FACE ( 'NONE', ( #90167 ), #47445, .F. ) ;
#115694=DIRECTION ( 'NONE',  ( -0.7071067811865486830, -0.7071067811865464625, 0.000000000000000000 ) ) ;
#115696=DIRECTION ( 'NONE',  ( -0.000000000000000000, -0.3543493200069152693, 0.9351131265310292928 ) ) ;
#115697=ORIENTED_EDGE ( 'NONE', *, *, #83627, .T. ) ;
#115698=CARTESIAN_POINT ( 'NONE',  ( 20.99999999999985079, -0.2811185226894094558, -5.995736974527563490 ) ) ;
#115699=ORIENTED_EDGE ( 'NONE', *, *, #41213, .T. ) ;
#115700=VECTOR ( 'NONE', #114256, 1000.000000000000000 ) ;
#115703=CARTESIAN_POINT ( 'NONE',  ( -51.18398860626899705, 28.73617430169823095, 5.000000000000000000 ) ) ;
#115704=VECTOR ( 'NONE', #134341, 1000.000000000000227 ) ;
#115705=DIRECTION ( 'NONE',  ( -0.7071067811865487940, 0.7071067811865463515, -0.000000000000000000 ) ) ;
#115706=CARTESIAN_POINT ( 'NONE',  ( -14.51078643762690490, -27.52281430457045275, 5.000000000000000000 ) ) ;
#115707=ORIENTED_EDGE ( 'NONE', *, *, #41124, .T. ) ;
#115708=AXIS2_PLACEMENT_3D ( 'NONE', #84321, #96549, #41485 ) ;
#115709=VECTOR ( 'NONE', #50106, 1000.000000000000227 ) ;
#115711=VECTOR ( 'NONE', #18431, 1000.000000000000000 ) ;
#115712=DIRECTION ( 'NONE',  ( -0.000000000000000000, 0.3543493200069153248, 0.9351131265310292928 ) ) ;
#115717=ORIENTED_EDGE ( 'NONE', *, *, #21201, .F. ) ;
#115719=DIRECTION ( 'NONE',  ( -0.7071067811865486830, -0.7071067811865464625, -0.000000000000000000 ) ) ;
#115720=AXIS2_PLACEMENT_3D ( 'NONE', #80279, #114976, #138931 ) ;
#115722=ORIENTED_EDGE ( 'NONE', *, *, #12870, .T. ) ;
#115723=ORIENTED_EDGE ( 'NONE', *, *, #12202, .F. ) ;
#115724=ORIENTED_EDGE ( 'NONE', *, *, #91262, .T. ) ;
#115726=ORIENTED_EDGE ( 'NONE', *, *, #66978, .T. ) ;
#115727=FACE_OUTER_BOUND ( 'NONE', #50686, .T. ) ;
#115728=LINE ( 'NONE', #81759, #115053 ) ;
#115729=VECTOR ( 'NONE', #67629, 999.9999999999998863 ) ;
#115730=VECTOR ( 'NONE', #46988, 1000.000000000000227 ) ;
#115731=LINE ( 'NONE', #6248, #15561 ) ;
#115733=ORIENTED_EDGE ( 'NONE', *, *, #120357, .F. ) ;
#115734=DIRECTION ( 'NONE',  ( 0.6830127018922180770, -0.6830127018922204085, -0.2588190451025213501 ) ) ;
#115735=DIRECTION ( 'NONE',  ( 0.7071067811865486830, -0.7071067811865464625, -0.000000000000000000 ) ) ;
#115736=VECTOR ( 'NONE', #74416, 1000.000000000000000 ) ;
#115737=ORIENTED_EDGE ( 'NONE', *, *, #119908, .F. ) ;
#115738=EDGE_CURVE ( 'NONE', #55801, #100675, #38659, .T. ) ;
#115739=LINE ( 'NONE', #60741, #7299 ) ;
#115740=VECTOR ( 'NONE', #124293, 1000.000000000000000 ) ;
#115741=DIRECTION ( 'NONE',  ( 0.7071067811865487940, -0.7071067811865463515, 0.000000000000000000 ) ) ;
#115742=DIRECTION ( 'NONE',  ( -0.000000000000000000, 0.000000000000000000, 1.000000000000000000 ) ) ;
#115743=VECTOR ( 'NONE', #5708, 1000.000000000000000 ) ;
#115744=ORIENTED_EDGE ( 'NONE', *, *, #136641, .T. ) ;
#115745=VERTEX_POINT ( 'NONE', #5980 ) ;
#115748=VECTOR ( 'NONE', #114271, 999.9999999999998863 ) ;
#115749=EDGE_CURVE ( 'NONE', #20953, #134952, #140797, .T. ) ;
#115750=DIRECTION ( 'NONE',  ( -0.3543493200069162685, -0.000000000000000000, -0.9351131265310288487 ) ) ;
#115751=FACE_OUTER_BOUND ( 'NONE', #14336, .T. ) ;
#115752=DIRECTION ( 'NONE',  ( -0.000000000000000000, 0.3543493200069153248, 0.9351131265310292928 ) ) ;
#115753=CARTESIAN_POINT ( 'NONE',  ( -8.999999999999937828, -3.485240976185084882, -4.108735105802418630 ) ) ;
#115755=PLANE ( 'NONE',  #55034 ) ;
#115756=DIRECTION ( 'NONE',  ( 0.7071067811865487940, 0.7071067811865463515, 0.000000000000000000 ) ) ;
#115757=VERTEX_POINT ( 'NONE', #50965 ) ;
#115759=EDGE_LOOP ( 'NONE', ( #75379, #53959, #69927, #132273 ) ) ;
#115760=ORIENTED_EDGE ( 'NONE', *, *, #38715, .F. ) ;
#115762=EDGE_CURVE ( 'NONE', #120761, #55777, #27054, .T. ) ;
#115763=CARTESIAN_POINT ( 'NONE',  ( -14.18650864602352080, -15.74070752338411694, 8.904080028138976033 ) ) ;
#115766=CARTESIAN_POINT ( 'NONE',  ( -45.29974487139158867, -27.71228299555237840, 4.000000000000000000 ) ) ;
#115767=CARTESIAN_POINT ( 'NONE',  ( 5.843876922607536883, -22.22500000000000497, 4.000000000000000000 ) ) ;
#115768=DIRECTION ( 'NONE',  ( -0.7071067811865487940, 0.7071067811865463515, -0.000000000000000000 ) ) ;
#115769=DIRECTION ( 'NONE',  ( -0.000000000000000000, 0.000000000000000000, 1.000000000000000000 ) ) ;
#115770=VECTOR ( 'NONE', #7591, 999.9999999999998863 ) ;
#115771=DIRECTION ( 'NONE',  ( 0.7071067811865486830, -0.7071067811865464625, -0.000000000000000000 ) ) ;
#115772=ORIENTED_EDGE ( 'NONE', *, *, #112530, .F. ) ;
#115773=DIRECTION ( 'NONE',  ( 1.000000000000000000, 0.000000000000000000, 0.000000000000000000 ) ) ;
#115774=CARTESIAN_POINT ( 'NONE',  ( 0.2917770898304763993, -15.74070752338411694, 19.73771281079097761 ) ) ;
#115775=EDGE_LOOP ( 'NONE', ( #61993, #36510, #56919, #136230 ) ) ;
#115776=ORIENTED_EDGE ( 'NONE', *, *, #135797, .F. ) ;
#115777=ORIENTED_EDGE ( 'NONE', *, *, #37822, .F. ) ;
#115778=DIRECTION ( 'NONE',  ( 0.6830127018922181881, 0.6830127018922202975, -0.2588190451025214056 ) ) ;
#115779=VERTEX_POINT ( 'NONE', #128530 ) ;
#115780=ORIENTED_EDGE ( 'NONE', *, *, #64035, .F. ) ;
#115782=VECTOR ( 'NONE', #35171, 999.9999999999998863 ) ;
#115783=VERTEX_POINT ( 'NONE', #117601 ) ;
#115784=VECTOR ( 'NONE', #2991, 1000.000000000000000 ) ;
#115786=DIRECTION ( 'NONE',  ( -0.7071067811865486830, -0.7071067811865464625, 0.000000000000000000 ) ) ;
#115787=EDGE_CURVE ( 'NONE', #3513, #62344, #137978, .T. ) ;
#115788=CARTESIAN_POINT ( 'NONE',  ( 24.48921356237309510, -27.52281430457072631, 5.000000000000000000 ) ) ;
#115790=PLANE ( 'NONE',  #5480 ) ;
#115791=EDGE_CURVE ( 'NONE', #39763, #128366, #5279, .T. ) ;
#115792=PLANE ( 'NONE',  #27748 ) ;
#115793=CARTESIAN_POINT ( 'NONE',  ( -16.49999999999988276, -13.91253812416061386, 4.000000000000000000 ) ) ;
#115794=CARTESIAN_POINT ( 'NONE',  ( -51.48921356237309510, -27.52281430457091460, 5.000000000000000000 ) ) ;
#115795=CARTESIAN_POINT ( 'NONE',  ( -12.75860074219786711, 21.72500000000000142, 5.000000000000000000 ) ) ;
#115796=VECTOR ( 'NONE', #84685, 1000.000000000000000 ) ;
#115798=EDGE_CURVE ( 'NONE', #134215, #122079, #29194, .T. ) ;
#115799=ADVANCED_FACE ( 'NONE', ( #41496 ), #95879, .F. ) ;
#115800=DIRECTION ( 'NONE',  ( -0.7071067811865487940, 0.7071067811865463515, -0.000000000000000000 ) ) ;
#115801=VECTOR ( 'NONE', #7915, 1000.000000000000000 ) ;
#115802=VECTOR ( 'NONE', #110412, 1000.000000000000227 ) ;
#115803=ORIENTED_EDGE ( 'NONE', *, *, #143162, .F. ) ;
#115804=VERTEX_POINT ( 'NONE', #72767 ) ;
#115805=VERTEX_POINT ( 'NONE', #126364 ) ;
#115807=AXIS2_PLACEMENT_3D ( 'NONE', #39396, #72051, #70628 ) ;
#115808=VECTOR ( 'NONE', #36725, 1000.000000000000000 ) ;
#115809=VERTEX_POINT ( 'NONE', #6686 ) ;
#115812=VECTOR ( 'NONE', #55222, 1000.000000000000000 ) ;
#115813=PLANE ( 'NONE',  #32925 ) ;
#115815=EDGE_CURVE ( 'NONE', #142125, #37121, #115455, .T. ) ;
#115816=CARTESIAN_POINT ( 'NONE',  ( -27.48921356237309155, -27.52281430457074762, 5.000000000000000000 ) ) ;
#115817=ADVANCED_FACE ( 'NONE', ( #16144 ), #60438, .F. ) ;
#115818=LINE ( 'NONE', #124594, #90391 ) ;
#115819=ORIENTED_EDGE ( 'NONE', *, *, #81730, .T. ) ;
#115820=CARTESIAN_POINT ( 'NONE',  ( 51.29974487139158867, -27.71228299555242103, 4.000000000000000000 ) ) ;
#115821=VECTOR ( 'NONE', #112370, 1000.000000000000000 ) ;
#115823=EDGE_CURVE ( 'NONE', #32796, #16078, #61175, .T. ) ;
#115825=LINE ( 'NONE', #60818, #81733 ) ;
#115826=DIRECTION ( 'NONE',  ( -0.6830127018922181881, 0.6830127018922202975, -0.2588190451025214056 ) ) ;
#115827=FACE_OUTER_BOUND ( 'NONE', #20285, .T. ) ;
#115829=EDGE_LOOP ( 'NONE', ( #39967, #108590, #115733, #34757 ) ) ;
#115831=CARTESIAN_POINT ( 'NONE',  ( -38.99451991528749062, 28.92564299267965211, 4.000000000000000000 ) ) ;
#115832=VECTOR ( 'NONE', #3559, 999.9999999999998863 ) ;
#115833=LINE ( 'NONE', #83250, #139043 ) ;
#115834=EDGE_CURVE ( 'NONE', #128651, #56450, #140128, .T. ) ;
#115837=LINE ( 'NONE', #77737, #6854 ) ;
#115838=DIRECTION ( 'NONE',  ( 0.7071067811865486830, -0.7071067811865464625, -0.000000000000000000 ) ) ;
#115839=VECTOR ( 'NONE', #37888, 1000.000000000000000 ) ;
#115840=VECTOR ( 'NONE', #50224, 1000.000000000000227 ) ;
#115841=DIRECTION ( 'NONE',  ( 0.7071067811865487940, -0.7071067811865463515, 0.000000000000000000 ) ) ;
#115842=FACE_OUTER_BOUND ( 'NONE', #135387, .T. ) ;
#115843=PLANE ( 'NONE',  #74329 ) ;
#115845=ORIENTED_EDGE ( 'NONE', *, *, #40735, .F. ) ;
#115846=LINE ( 'NONE', #15802, #27910 ) ;
#115848=DIRECTION ( 'NONE',  ( 0.000000000000000000, 0.000000000000000000, 1.000000000000000000 ) ) ;
#115849=VECTOR ( 'NONE', #88816, 1000.000000000000000 ) ;
#115850=ORIENTED_EDGE ( 'NONE', *, *, #96517, .T. ) ;
#115851=CARTESIAN_POINT ( 'NONE',  ( 0.4892135623730947680, -27.52281430457055578, 5.000000000000000000 ) ) ;
#115852=DIRECTION ( 'NONE',  ( -0.000000000000000000, 0.000000000000000000, 1.000000000000000000 ) ) ;
#115853=ORIENTED_EDGE ( 'NONE', *, *, #67032, .F. ) ;
#115854=ORIENTED_EDGE ( 'NONE', *, *, #63774, .F. ) ;
#115856=DIRECTION ( 'NONE',  ( -0.7071067811865487940, 0.7071067811865463515, 0.000000000000000000 ) ) ;
#115857=EDGE_CURVE ( 'NONE', #4377, #139589, #27770, .T. ) ;
#115858=DIRECTION ( 'NONE',  ( 0.6830127018922181881, 0.6830127018922202975, -0.2588190451025214056 ) ) ;
#115859=EDGE_CURVE ( 'NONE', #89571, #21371, #39385, .T. ) ;
#115863=VERTEX_POINT ( 'NONE', #28507 ) ;
#115864=CARTESIAN_POINT ( 'NONE',  ( -42.18398860626899705, 28.73617430169816700, 5.000000000000000000 ) ) ;
#115865=LINE ( 'NONE', #16565, #36951 ) ;
#115866=EDGE_CURVE ( 'NONE', #34536, #112793, #116921, .T. ) ;
#115868=DIRECTION ( 'NONE',  ( 0.6830127018922181881, 0.6830127018922202975, -0.2588190451025214056 ) ) ;
#115869=AXIS2_PLACEMENT_3D ( 'NONE', #114954, #15635, #59922 ) ;
#115870=CARTESIAN_POINT ( 'NONE',  ( 57.18398860626899705, 28.73617430169827358, 5.000000000000000000 ) ) ;
#115872=LINE ( 'NONE', #50648, #70377 ) ;
#115873=FACE_OUTER_BOUND ( 'NONE', #74491, .T. ) ;
#115875=VECTOR ( 'NONE', #40002, 1000.000000000000227 ) ;
#115877=CARTESIAN_POINT ( 'NONE',  ( -36.29974487139159578, -27.71228299555231445, 4.000000000000000000 ) ) ;
#115880=ORIENTED_EDGE ( 'NONE', *, *, #4492, .F. ) ;
#115884=ORIENTED_EDGE ( 'NONE', *, *, #115671, .T. ) ;
#115885=ORIENTED_EDGE ( 'NONE', *, *, #27161, .F. ) ;
#115886=DIRECTION ( 'NONE',  ( 0.7071067811865486830, -0.7071067811865464625, -0.000000000000000000 ) ) ;
#115887=DIRECTION ( 'NONE',  ( -0.3543493200069162685, -0.000000000000000000, -0.9351131265310288487 ) ) ;
#115889=CARTESIAN_POINT ( 'NONE',  ( -19.82816939922339472, -11.24070752338416490, 4.000000000000000000 ) ) ;
#115890=EDGE_LOOP ( 'NONE', ( #120325, #5728, #91120, #66235 ) ) ;
#115891=CARTESIAN_POINT ( 'NONE',  ( -39.29974487139159578, -27.71228299555233576, 4.000000000000000000 ) ) ;
#115893=CARTESIAN_POINT ( 'NONE',  ( -27.79289321881325847, -14.24070752338414003, 5.000000000000000000 ) ) ;
#115894=CARTESIAN_POINT ( 'NONE',  ( 21.29974487139158512, -27.71228299555221142, 4.000000000000000000 ) ) ;
#115895=CARTESIAN_POINT ( 'NONE',  ( 11.27718569542934191, -21.72500000000000853, 5.000000000000000000 ) ) ;
#115896=CYLINDRICAL_SURFACE ( 'NONE', #95975, 5.968999999999998529 ) ;
#115898=CARTESIAN_POINT ( 'NONE',  ( -53.99451991528749062, 28.92564299267975869, 4.000000000000000000 ) ) ;
#115899=VECTOR ( 'NONE', #56044, 1000.000000000000000 ) ;
#115900=CARTESIAN_POINT ( 'NONE',  ( -48.18398860626899705, 28.73617430169820608, 5.000000000000000000 ) ) ;
#115902=VECTOR ( 'NONE', #41325, 1000.000000000000227 ) ;
#115903=FACE_OUTER_BOUND ( 'NONE', #55505, .T. ) ;
#115905=ORIENTED_EDGE ( 'NONE', *, *, #95606, .F. ) ;
#115906=ORIENTED_EDGE ( 'NONE', *, *, #132031, .T. ) ;
#115908=ORIENTED_EDGE ( 'NONE', *, *, #71713, .F. ) ;
#115910=LINE ( 'NONE', #39103, #75685 ) ;
#115911=DIRECTION ( 'NONE',  ( -0.7071067811865486830, -0.7071067811865464625, 0.000000000000000000 ) ) ;
#115912=ORIENTED_EDGE ( 'NONE', *, *, #85351, .F. ) ;
#115913=VECTOR ( 'NONE', #128046, 1000.000000000000000 ) ;
#115915=VECTOR ( 'NONE', #117217, 1000.000000000000227 ) ;
#115916=VECTOR ( 'NONE', #60006, 1000.000000000000000 ) ;
#115918=ORIENTED_EDGE ( 'NONE', *, *, #34532, .T. ) ;
#115919=DIRECTION ( 'NONE',  ( 0.7071067811865487940, 0.7071067811865463515, 0.000000000000000000 ) ) ;
#115921=DIRECTION ( 'NONE',  ( -1.000000000000000000, 3.640042140494138811E-14, 0.000000000000000000 ) ) ;
#115922=VECTOR ( 'NONE', #12447, 1000.000000000000000 ) ;
#115923=CIRCLE ( 'NONE', #53449, 5.968999999999998529 ) ;
#115925=AXIS2_PLACEMENT_3D ( 'NONE', #111988, #133039, #77927 ) ;
#115927=CARTESIAN_POINT ( 'NONE',  ( -33.48921356237309510, -27.52281430457078670, 5.000000000000000000 ) ) ;
#115929=VECTOR ( 'NONE', #6860, 1000.000000000000000 ) ;
#115930=VERTEX_POINT ( 'NONE', #19748 ) ;
#115931=ORIENTED_EDGE ( 'NONE', *, *, #9175, .F. ) ;
#115932=EDGE_CURVE ( 'NONE', #46130, #40296, #44397, .T. ) ;
#115933=ORIENTED_EDGE ( 'NONE', *, *, #14861, .F. ) ;
#115935=ADVANCED_FACE ( 'NONE', ( #129950 ), #55248, .F. ) ;
#115936=PLANE ( 'NONE',  #114789 ) ;
#115938=AXIS2_PLACEMENT_3D ( 'NONE', #119307, #108402, #73684 ) ;
#115941=EDGE_LOOP ( 'NONE', ( #139875, #103080, #18917, #51369 ) ) ;
#115942=EDGE_CURVE ( 'NONE', #39257, #47204, #88602, .T. ) ;
#115943=VERTEX_POINT ( 'NONE', #74882 ) ;
#115945=CARTESIAN_POINT ( 'NONE',  ( -39.18398860626899705, 28.73617430169814568, 5.000000000000000000 ) ) ;
#115946=VERTEX_POINT ( 'NONE', #33519 ) ;
#115947=ORIENTED_EDGE ( 'NONE', *, *, #95007, .F. ) ;
#115948=VECTOR ( 'NONE', #102709, 999.9999999999998863 ) ;
#115950=EDGE_CURVE ( 'NONE', #120720, #91343, #100182, .T. ) ;
#115951=AXIS2_PLACEMENT_3D ( 'NONE', #43078, #65567, #56112 ) ;
#115952=VECTOR ( 'NONE', #192, 1000.000000000000000 ) ;
#115953=CARTESIAN_POINT ( 'NONE',  ( -12.70710678118645909, 17.25929247661554200, 5.000000000000000000 ) ) ;
#115954=LINE ( 'NONE', #18048, #109667 ) ;
#115956=CARTESIAN_POINT ( 'NONE',  ( 2.292986735706931345, -21.74070752338405654, 4.999753212805221558 ) ) ;
#115957=VECTOR ( 'NONE', #12051, 1000.000000000000000 ) ;
#115958=CARTESIAN_POINT ( 'NONE',  ( 26.29298673570676215, -21.74070752338406365, 4.999753212805220670 ) ) ;
#115959=LINE ( 'NONE', #16663, #32149 ) ;
#115960=EDGE_CURVE ( 'NONE', #1441, #58822, #65434, .T. ) ;
#115961=VECTOR ( 'NONE', #1570, 1000.000000000000000 ) ;
#115963=EDGE_LOOP ( 'NONE', ( #81024, #40224, #129351, #101023 ) ) ;
#115964=FACE_BOUND ( 'NONE', #59128, .T. ) ;
#115965=ORIENTED_EDGE ( 'NONE', *, *, #90285, .F. ) ;
#115966=LINE ( 'NONE', #16670, #48083 ) ;
#115970=LINE ( 'NONE', #13796, #45846 ) ;
#115971=EDGE_LOOP ( 'NONE', ( #77652, #125956, #106876, #66592 ) ) ;
#115972=ORIENTED_EDGE ( 'NONE', *, *, #95185, .T. ) ;
#115973=EDGE_CURVE ( 'NONE', #101734, #111455, #108866, .T. ) ;
#115974=EDGE_LOOP ( 'NONE', ( #18495, #15721, #55251, #40683 ) ) ;
#115978=CARTESIAN_POINT ( 'NONE',  ( 18.79333936457835108, 21.75929247661549937, 4.998822639870708073 ) ) ;
#115980=DIRECTION ( 'NONE',  ( -0.7071067811865486830, -0.7071067811865464625, 0.000000000000000000 ) ) ;
#115981=EDGE_CURVE ( 'NONE', #88273, #133448, #99428, .T. ) ;
#115982=LINE ( 'NONE', #80549, #56121 ) ;
#115983=AXIS2_PLACEMENT_3D ( 'NONE', #136076, #46995, #114322 ) ;
#115984=VECTOR ( 'NONE', #66512, 1000.000000000000227 ) ;
#115985=FACE_OUTER_BOUND ( 'NONE', #25380, .T. ) ;
#115986=EDGE_CURVE ( 'NONE', #98221, #98945, #119057, .T. ) ;
#115987=EDGE_CURVE ( 'NONE', #118822, #28861, #108152, .T. ) ;
#115988=DIRECTION ( 'NONE',  ( 0.7071067811865487940, 0.7071067811865463515, 0.000000000000000000 ) ) ;
#115989=DIRECTION ( 'NONE',  ( -0.6830127018922181881, 0.6830127018922202975, -0.2588190451025214056 ) ) ;
#115990=DIRECTION ( 'NONE',  ( 0.7071067811865486830, -0.7071067811865464625, -0.000000000000000000 ) ) ;
#115991=LINE ( 'NONE', #70427, #72634 ) ;
#115993=ORIENTED_EDGE ( 'NONE', *, *, #100100, .T. ) ;
#115994=EDGE_LOOP ( 'NONE', ( #100916, #74185, #75204, #90390 ) ) ;
#115995=ORIENTED_EDGE ( 'NONE', *, *, #111228, .T. ) ;
#115996=AXIS2_PLACEMENT_3D ( 'NONE', #14408, #3496, #47789 ) ;
#115997=EDGE_LOOP ( 'NONE', ( #124283, #75457, #95758, #14448 ) ) ;
#115998=FACE_OUTER_BOUND ( 'NONE', #129982, .T. ) ;
#115999=ORIENTED_EDGE ( 'NONE', *, *, #109562, .F. ) ;
#116000=ADVANCED_FACE ( 'NONE', ( #8817 ), #54548, .F. ) ;
#116001=VERTEX_POINT ( 'NONE', #98725 ) ;
#116002=CYLINDRICAL_SURFACE ( 'NONE', #123146, 0.5000000000000004441 ) ;
#116003=DIRECTION ( 'NONE',  ( -0.000000000000000000, -0.000000000000000000, 1.000000000000000000 ) ) ;
#116004=ADVANCED_FACE ( 'NONE', ( #42957 ), #53075, .F. ) ;
#116005=EDGE_CURVE ( 'NONE', #49326, #140411, #22568, .T. ) ;
#116006=CARTESIAN_POINT ( 'NONE',  ( 19.36246187583889977, 22.22499999999999432, 4.000000000000000000 ) ) ;
#116007=ORIENTED_EDGE ( 'NONE', *, *, #116236, .T. ) ;
#116008=FACE_OUTER_BOUND ( 'NONE', #101510, .T. ) ;
#116009=AXIS2_PLACEMENT_3D ( 'NONE', #113227, #69781, #25505 ) ;
#116011=DIRECTION ( 'NONE',  ( -0.7071067811865486830, -0.7071067811865464625, 0.000000000000000000 ) ) ;
#116012=CARTESIAN_POINT ( 'NONE',  ( 34.49999999999975131, 9.054329344830847504, 4.994342998332164107 ) ) ;
#116014=ORIENTED_EDGE ( 'NONE', *, *, #120968, .T. ) ;
#116016=DIRECTION ( 'NONE',  ( 0.3543493200069162685, -0.000000000000000000, -0.9351131265310288487 ) ) ;
#116017=EDGE_CURVE ( 'NONE', #115415, #110261, #11696, .T. ) ;
#116018=PLANE ( 'NONE',  #339 ) ;
#116019=DIRECTION ( 'NONE',  ( 0.7071067811865487940, 0.7071067811865463515, -0.000000000000000000 ) ) ;
#116021=ORIENTED_EDGE ( 'NONE', *, *, #54144, .T. ) ;
#116022=PLANE ( 'NONE',  #28766 ) ;
#116025=LINE ( 'NONE', #83435, #32433 ) ;
#116028=ADVANCED_FACE ( 'NONE', ( #86456 ), #87153, .F. ) ;
#116029=FACE_OUTER_BOUND ( 'NONE', #100679, .T. ) ;
#116031=( BOUNDED_CURVE ( )  B_SPLINE_CURVE ( 3, ( #139678, #71545, #62102, #106261 ),
 .UNSPECIFIED., .F., .F. ) 
 B_SPLINE_CURVE_WITH_KNOTS ( ( 4, 4 ),
 ( 1.739935637444958161, 1.766022064991929152 ),
 .UNSPECIFIED. ) 
 CURVE ( )  GEOMETRIC_REPRESENTATION_ITEM ( )  RATIONAL_B_SPLINE_CURVE ( ( 1.000000000000000000, 0.9999432923287778774, 0.9999432923287778774, 1.000000000000000000 ) ) 
 REPRESENTATION_ITEM ( '' )  );
#116034=FACE_OUTER_BOUND ( 'NONE', #70713, .T. ) ;
#116036=LINE ( 'NONE', #38502, #48810 ) ;
#116037=DIRECTION ( 'NONE',  ( -0.000000000000000000, -0.3543493200069152693, 0.9351131265310292928 ) ) ;
#116038=EDGE_LOOP ( 'NONE', ( #140871, #39371, #78950, #59964 ) ) ;
#116039=FACE_OUTER_BOUND ( 'NONE', #39677, .T. ) ;
#116041=AXIS2_PLACEMENT_3D ( 'NONE', #143184, #109122, #87389 ) ;
#116042=VECTOR ( 'NONE', #8678, 1000.000000000000000 ) ;
#116043=VECTOR ( 'NONE', #124520, 1000.000000000000000 ) ;
#116044=CARTESIAN_POINT ( 'NONE',  ( 0.005480084712502889671, 28.92564299267938210, 4.000000000000000000 ) ) ;
#116045=VECTOR ( 'NONE', #76292, 1000.000000000000227 ) ;
#116049=ORIENTED_EDGE ( 'NONE', *, *, #43035, .F. ) ;
#116050=DIRECTION ( 'NONE',  ( 0.7071067811865486830, -0.7071067811865464625, -0.000000000000000000 ) ) ;
#116052=CARTESIAN_POINT ( 'NONE',  ( -34.92500000000001137, -19.19990548397260000, 4.759050581649338696 ) ) ;
#116053=ORIENTED_EDGE ( 'NONE', *, *, #89951, .T. ) ;
#116054=LINE ( 'NONE', #26216, #72013 ) ;
#116056=EDGE_CURVE ( 'NONE', #38115, #751, #66138, .T. ) ;
#116057=CARTESIAN_POINT ( 'NONE',  ( 27.48921356237309155, -27.52281430457074762, 5.000000000000000000 ) ) ;
#116058=EDGE_CURVE ( 'NONE', #25180, #99905, #120448, .T. ) ;
#116060=ORIENTED_EDGE ( 'NONE', *, *, #133450, .T. ) ;
#116061=AXIS2_PLACEMENT_3D ( 'NONE', #101902, #118479, #27185 ) ;
#116063=LINE ( 'NONE', #18147, #69783 ) ;
#116064=CARTESIAN_POINT ( 'NONE',  ( -47.99451991528749062, 28.92564299267971251, 4.000000000000000000 ) ) ;
#116068=CARTESIAN_POINT ( 'NONE',  ( -9.328169399223463998, -3.740707523384244837, 4.000000000000000000 ) ) ;
#116070=DIRECTION ( 'NONE',  ( 0.6830127018922181881, 0.6830127018922202975, -0.2588190451025214056 ) ) ;
#116071=ORIENTED_EDGE ( 'NONE', *, *, #79276, .F. ) ;
#116072=VECTOR ( 'NONE', #31139, 1000.000000000000000 ) ;
#116073=ORIENTED_EDGE ( 'NONE', *, *, #76462, .T. ) ;
#116074=ORIENTED_EDGE ( 'NONE', *, *, #124626, .F. ) ;
#116076=VECTOR ( 'NONE', #128109, 1000.000000000000000 ) ;
#116077=VERTEX_POINT ( 'NONE', #89297 ) ;
#116078=ORIENTED_EDGE ( 'NONE', *, *, #115791, .T. ) ;
#116079=VERTEX_POINT ( 'NONE', #58868 ) ;
#116080=FACE_OUTER_BOUND ( 'NONE', #97732, .T. ) ;
#116081=LINE ( 'NONE', #106607, #94842 ) ;
#116082=VERTEX_POINT ( 'NONE', #134971 ) ;
#116083=PLANE ( 'NONE',  #9145 ) ;
#116084=CARTESIAN_POINT ( 'NONE',  ( 1.961882696559495765, 22.22500000000000142, 18.97781875781104333 ) ) ;
#116085=DIRECTION ( 'NONE',  ( -0.7071067811865486830, -0.7071067811865464625, 0.000000000000000000 ) ) ;
#116088=VECTOR ( 'NONE', #51202, 1000.000000000000000 ) ;
#116089=ORIENTED_EDGE ( 'NONE', *, *, #48883, .T. ) ;
#116091=DIRECTION ( 'NONE',  ( -0.000000000000000000, -0.3543493200069152693, 0.9351131265310292928 ) ) ;
#116092=LINE ( 'NONE', #71196, #45113 ) ;
#116093=DIRECTION ( 'NONE',  ( -0.000000000000000000, 0.3543493200069153248, 0.9351131265310292928 ) ) ;
#116095=LINE ( 'NONE', #128425, #35345 ) ;
#116097=CARTESIAN_POINT ( 'NONE',  ( 27.29974487139158512, -27.71228299555225405, 4.000000000000000000 ) ) ;
#116098=PLANE ( 'NONE',  #60018 ) ;
#116099=EDGE_LOOP ( 'NONE', ( #127594, #58290, #125504, #133105 ) ) ;
#116100=EDGE_LOOP ( 'NONE', ( #40072, #95762, #25233, #55559 ) ) ;
#116102=EDGE_LOOP ( 'NONE', ( #120407, #140694, #95237, #124046, #127785 ) ) ;
#116103=CARTESIAN_POINT ( 'NONE',  ( -17.51078643762690845, -27.52281430457043143, 5.000000000000000000 ) ) ;
#116104=ADVANCED_FACE ( 'NONE', ( #123378 ), #103702, .F. ) ;
#116105=ADVANCED_FACE ( 'NONE', ( #25444 ), #45119, .T. ) ;
#116106=VECTOR ( 'NONE', #70534, 1000.000000000000000 ) ;
#116107=CARTESIAN_POINT ( 'NONE',  ( -26.99999999999981526, -18.41253812416056945, 4.000000000000000000 ) ) ;
#116108=VERTEX_POINT ( 'NONE', #35670 ) ;
#116109=VECTOR ( 'NONE', #8847, 1000.000000000000000 ) ;
#116110=CARTESIAN_POINT ( 'NONE',  ( 34.49999999999975842, -19.53574439159931231, 4.994342998332164107 ) ) ;
#116115=ORIENTED_EDGE ( 'NONE', *, *, #59276, .T. ) ;
#116117=DIRECTION ( 'NONE',  ( -0.7071067811865486830, -0.7071067811865464625, 0.000000000000000000 ) ) ;
#116118=ORIENTED_EDGE ( 'NONE', *, *, #34550, .F. ) ;
#116120=FACE_OUTER_BOUND ( 'NONE', #41141, .T. ) ;
#116121=CARTESIAN_POINT ( 'NONE',  ( -23.52663903635771092, -5.240707523384225297, 16.25846745537490179 ) ) ;
#116122=LINE ( 'NONE', #97956, #72241 ) ;
#116127=EDGE_CURVE ( 'NONE', #88880, #49293, #2620, .T. ) ;
#116128=EDGE_CURVE ( 'NONE', #80339, #84583, #90744, .T. ) ;
#116130=CARTESIAN_POINT ( 'NONE',  ( 0.000000000000000000, 0.000000000000000000, 5.000000000000000000 ) ) ;
#116131=DIRECTION ( 'NONE',  ( -0.7071067811865486830, 0.7071067811865464625, 0.000000000000000000 ) ) ;
#116133=DIRECTION ( 'NONE',  ( -0.7071067811865486830, -0.7071067811865464625, 0.000000000000000000 ) ) ;
#116135=EDGE_CURVE ( 'NONE', #1016, #98487, #92128, .T. ) ;
#116136=ADVANCED_FACE ( 'NONE', ( #34932 ), #125501, .F. ) ;
#116138=ORIENTED_EDGE ( 'NONE', *, *, #70760, .T. ) ;
#116139=CARTESIAN_POINT ( 'NONE',  ( -9.792893218813388145, 3.759292476615671230, 5.000000000000000000 ) ) ;
#116140=EDGE_CURVE ( 'NONE', #105421, #136452, #122623, .T. ) ;
#116142=VERTEX_POINT ( 'NONE', #57401 ) ;
#116143=ORIENTED_EDGE ( 'NONE', *, *, #15901, .F. ) ;
#116144=LINE ( 'NONE', #82136, #30758 ) ;
#116146=AXIS2_PLACEMENT_3D ( 'NONE', #135654, #102329, #47270 ) ;
#116149=EDGE_CURVE ( 'NONE', #128263, #118475, #47277, .T. ) ;
#116151=DIRECTION ( 'NONE',  ( -0.7071067811865486830, 0.7071067811865464625, 0.000000000000000000 ) ) ;
#116152=VERTEX_POINT ( 'NONE', #1531 ) ;
#116154=EDGE_CURVE ( 'NONE', #104818, #139610, #2243, .T. ) ;
#116155=VECTOR ( 'NONE', #107680, 1000.000000000000000 ) ;
#116156=VECTOR ( 'NONE', #107863, 1000.000000000000000 ) ;
#116159=EDGE_CURVE ( 'NONE', #46535, #98731, #134237, .T. ) ;
#116160=VECTOR ( 'NONE', #94929, 999.9999999999998863 ) ;
#116161=CARTESIAN_POINT ( 'NONE',  ( 14.99999999999989875, 13.55218569542902429, 5.000000000000000000 ) ) ;
#116162=FACE_BOUND ( 'NONE', #15972, .T. ) ;
#116163=CARTESIAN_POINT ( 'NONE',  ( -8.510786437626906675, -27.52281430457049183, 5.000000000000000000 ) ) ;
#116164=DIRECTION ( 'NONE',  ( 0.7071067811865487940, 0.7071067811865463515, 0.000000000000000000 ) ) ;
#116165=DIRECTION ( 'NONE',  ( -0.7071067811865486830, -0.7071067811865464625, 0.000000000000000000 ) ) ;
#116166=ORIENTED_EDGE ( 'NONE', *, *, #53385, .T. ) ;
#116169=CARTESIAN_POINT ( 'NONE',  ( 0.000000000000000000, -21.72500000000000142, 4.500000000000000888 ) ) ;
#116170=ORIENTED_EDGE ( 'NONE', *, *, #80035, .F. ) ;
#116172=ORIENTED_EDGE ( 'NONE', *, *, #93148, .T. ) ;
#116173=DIRECTION ( 'NONE',  ( -0.6830127018922181881, 0.6830127018922202975, -0.2588190451025214056 ) ) ;
#116175=VERTEX_POINT ( 'NONE', #13130 ) ;
#116177=VERTEX_POINT ( 'NONE', #91450 ) ;
#116178=CARTESIAN_POINT ( 'NONE',  ( -29.99451991528749417, 28.92564299267958816, 4.000000000000000000 ) ) ;
#116179=CARTESIAN_POINT ( 'NONE',  ( -30.48921356237309510, -27.52281430457076894, 5.000000000000000000 ) ) ;
#116180=ADVANCED_FACE ( 'NONE', ( #101581 ), #46555, .F. ) ;
#116181=EDGE_LOOP ( 'NONE', ( #70353, #97634, #101077, #117966 ) ) ;
#116182=LINE ( 'NONE', #61150, #137010 ) ;
#116185=VECTOR ( 'NONE', #21303, 1000.000000000000227 ) ;
#116186=CARTESIAN_POINT ( 'NONE',  ( 11.99999999999992006, -22.06887692260758982, 4.000000000000000000 ) ) ;
#116187=CARTESIAN_POINT ( 'NONE',  ( 0.000000000000000000, 0.000000000000000000, 5.000000000000000000 ) ) ;
#116188=DIRECTION ( 'NONE',  ( -0.7071067811865486830, -0.7071067811865464625, 0.000000000000000000 ) ) ;
#116189=ADVANCED_FACE ( 'NONE', ( #124773 ), #68988, .F. ) ;
#116190=VECTOR ( 'NONE', #84824, 1000.000000000000000 ) ;
#116192=DIRECTION ( 'NONE',  ( -0.6830127018922181881, 0.6830127018922202975, -0.2588190451025214056 ) ) ;
#116193=EDGE_LOOP ( 'NONE', ( #97184, #81931, #137314, #98312, #56002 ) ) ;
#116195=VECTOR ( 'NONE', #28027, 999.9999999999998863 ) ;
#116196=CARTESIAN_POINT ( 'NONE',  ( 33.32816939922329880, 2.259292476615694323, 4.000000000000000000 ) ) ;
#116197=CARTESIAN_POINT ( 'NONE',  ( -19.05000000000000071, 3.174999999999997158, 4.000000000000000000 ) ) ;
#116200=ORIENTED_EDGE ( 'NONE', *, *, #10689, .T. ) ;
#116202=DIRECTION ( 'NONE',  ( 0.7071067811865487940, -0.7071067811865463515, 0.000000000000000000 ) ) ;
#116205=ORIENTED_EDGE ( 'NONE', *, *, #36277, .F. ) ;
#116206=CARTESIAN_POINT ( 'NONE',  ( -8.994519915287490619, 28.92564299267944250, 4.000000000000000000 ) ) ;
#116207=VECTOR ( 'NONE', #69865, 1000.000000000000227 ) ;
#116208=CARTESIAN_POINT ( 'NONE',  ( 30.18398860626900060, 28.73617430169808173, 5.000000000000000000 ) ) ;
#116210=FACE_OUTER_BOUND ( 'NONE', #64818, .T. ) ;
#116211=ORIENTED_EDGE ( 'NONE', *, *, #8038, .T. ) ;
#116213=DIRECTION ( 'NONE',  ( 0.7071067811865486830, -0.7071067811865464625, -0.000000000000000000 ) ) ;
#116214=AXIS2_PLACEMENT_3D ( 'NONE', #15022, #113628, #81031 ) ;
#116215=LINE ( 'NONE', #125678, #59126 ) ;
#116218=DIRECTION ( 'NONE',  ( -0.000000000000000000, -0.3543493200069152693, 0.9351131265310292928 ) ) ;
#116220=ORIENTED_EDGE ( 'NONE', *, *, #5979, .F. ) ;
#116222=EDGE_CURVE ( 'NONE', #28440, #24958, #63120, .T. ) ;
#116226=CARTESIAN_POINT ( 'NONE',  ( 32.99999999999976552, 10.55218569542905982, 5.000000000000000000 ) ) ;
#116227=CARTESIAN_POINT ( 'NONE',  ( 21.18398860626899349, 28.73617430169802134, 5.000000000000000000 ) ) ;
#116228=PLANE ( 'NONE',  #25890 ) ;
#116229=AXIS2_PLACEMENT_3D ( 'NONE', #79189, #87880, #69005 ) ;
#116231=DIRECTION ( 'NONE',  ( -0.000000000000000000, -0.3543493200069152693, 0.9351131265310292928 ) ) ;
#116232=DIRECTION ( 'NONE',  ( -0.7071067811865487940, 0.7071067811865463515, 0.000000000000000000 ) ) ;
#116233=LINE ( 'NONE', #61194, #79356 ) ;
#116236=EDGE_CURVE ( 'NONE', #63701, #107149, #6507, .T. ) ;
#116237=ORIENTED_EDGE ( 'NONE', *, *, #37126, .F. ) ;
#116239=CARTESIAN_POINT ( 'NONE',  ( -23.91685193227054640, 21.75929247661549581, 7.311836541447997107 ) ) ;
#116242=LINE ( 'NONE', #27084, #36621 ) ;
#116243=EDGE_CURVE ( 'NONE', #82235, #112523, #92848, .T. ) ;
#116244=DIRECTION ( 'NONE',  ( -0.000000000000000000, 0.000000000000000000, 1.000000000000000000 ) ) ;
#116245=DIRECTION ( 'NONE',  ( -0.3543493200069162685, -0.000000000000000000, -0.9351131265310288487 ) ) ;
#116246=CARTESIAN_POINT ( 'NONE',  ( 7.499999999999949374, 15.05218569542901896, 5.000000000000000000 ) ) ;
#116247=ORIENTED_EDGE ( 'NONE', *, *, #38294, .T. ) ;
#116248=FACE_OUTER_BOUND ( 'NONE', #3033, .T. ) ;
#116249=CARTESIAN_POINT ( 'NONE',  ( 63.18398860626900415, 28.73617430169831621, 5.000000000000000000 ) ) ;
#116250=DIRECTION ( 'NONE',  ( 0.7071067811865487940, 0.7071067811865463515, 0.000000000000000000 ) ) ;
#116251=VECTOR ( 'NONE', #79375, 1000.000000000000000 ) ;
#116252=VECTOR ( 'NONE', #124532, 1000.000000000000000 ) ;
#116253=CARTESIAN_POINT ( 'NONE',  ( 0.000000000000000000, 0.000000000000000000, 5.000000000000000000 ) ) ;
#116257=ADVANCED_FACE ( 'NONE', ( #137814 ), #116018, .F. ) ;
#116258=ORIENTED_EDGE ( 'NONE', *, *, #39956, .T. ) ;
#116259=CARTESIAN_POINT ( 'NONE',  ( 0.005480084712502889671, 28.92564299267938210, 4.000000000000000000 ) ) ;
#116260=EDGE_LOOP ( 'NONE', ( #22477, #141038, #117500, #119496 ) ) ;
#116261=ORIENTED_EDGE ( 'NONE', *, *, #108913, .T. ) ;
#116262=AXIS2_PLACEMENT_3D ( 'NONE', #103259, #114145, #23569 ) ;
#116263=AXIS2_PLACEMENT_3D ( 'NONE', #118396, #74204, #64041 ) ;
#116264=LINE ( 'NONE', #115498, #1455 ) ;
#116265=CARTESIAN_POINT ( 'NONE',  ( -17.48334561358942807, 22.22500000000000142, 4.500000000000000888 ) ) ;
#116266=LINE ( 'NONE', #6735, #120581 ) ;
#116267=FACE_OUTER_BOUND ( 'NONE', #124692, .T. ) ;
#116268=EDGE_CURVE ( 'NONE', #83399, #37537, #50787, .T. ) ;
#116269=PLANE ( 'NONE',  #4724 ) ;
#116270=DIRECTION ( 'NONE',  ( -0.7071067811865486830, 0.7071067811865464625, 0.000000000000000000 ) ) ;
#116272=CARTESIAN_POINT ( 'NONE',  ( 12.18398860626900060, 28.73617430169795739, 5.000000000000000000 ) ) ;
#116273=CARTESIAN_POINT ( 'NONE',  ( -45.18398860626900415, 28.73617430169818832, 5.000000000000000000 ) ) ;
#116274=CARTESIAN_POINT ( 'NONE',  ( -34.75611968250421313, -15.18706574529247000, 4.955485411084893599 ) ) ;
#116275=DIRECTION ( 'NONE',  ( -0.6830127018922181881, 0.6830127018922202975, -0.2588190451025214056 ) ) ;
#116276=CARTESIAN_POINT ( 'NONE',  ( 34.49999999999975842, 6.054329344830883031, 4.994342998332162331 ) ) ;
#116278=DIRECTION ( 'NONE',  ( 0.6830127018922181881, 0.6830127018922202975, -0.2588190451025214056 ) ) ;
#116279=VERTEX_POINT ( 'NONE', #51516 ) ;
#116280=ORIENTED_EDGE ( 'NONE', *, *, #45221, .F. ) ;
#116283=DIRECTION ( 'NONE',  ( 0.7071067811865486830, -0.7071067811865464625, -0.000000000000000000 ) ) ;
#116284=ORIENTED_EDGE ( 'NONE', *, *, #615, .T. ) ;
#116285=VECTOR ( 'NONE', #42041, 1000.000000000000227 ) ;
#116286=LINE ( 'NONE', #137346, #37534 ) ;
#116287=DIRECTION ( 'NONE',  ( -0.7071067811865487940, 0.7071067811865463515, 0.000000000000000000 ) ) ;
#116289=AXIS2_PLACEMENT_3D ( 'NONE', #70093, #124418, #48284 ) ;
#116291=LINE ( 'NONE', #8892, #124375 ) ;
#116292=ORIENTED_EDGE ( 'NONE', *, *, #128350, .T. ) ;
#116293=ORIENTED_EDGE ( 'NONE', *, *, #138786, .T. ) ;
#116294=VECTOR ( 'NONE', #45724, 1000.000000000000114 ) ;
#116295=PLANE ( 'NONE',  #130285 ) ;
#116297=LINE ( 'NONE', #59797, #85961 ) ;
#116299=LINE ( 'NONE', #84414, #139187 ) ;
#116301=EDGE_CURVE ( 'NONE', #44113, #60323, #83469, .T. ) ;
#116303=ORIENTED_EDGE ( 'NONE', *, *, #134173, .F. ) ;
#116304=CARTESIAN_POINT ( 'NONE',  ( 22.49999999999985434, 16.18958161055405043, -11.56426086740806269 ) ) ;
#116305=PLANE ( 'NONE',  #87010 ) ;
#116308=CARTESIAN_POINT ( 'NONE',  ( 24.18398860626899705, 28.73617430169804265, 5.000000000000000000 ) ) ;
#116309=EDGE_CURVE ( 'NONE', #87414, #95968, #84163, .T. ) ;
#116310=ORIENTED_EDGE ( 'NONE', *, *, #25966, .T. ) ;
#116312=VERTEX_POINT ( 'NONE', #120279 ) ;
#116313=ADVANCED_FACE ( 'NONE', ( #31888 ), #52891, .F. ) ;
#116315=CARTESIAN_POINT ( 'NONE',  ( 8.510786437626906675, -27.52281430457049183, 5.000000000000000000 ) ) ;
#116316=ADVANCED_FACE ( 'NONE', ( #20995 ), #109443, .F. ) ;
#116320=VERTEX_POINT ( 'NONE', #65258 ) ;
#116321=VERTEX_POINT ( 'NONE', #74706 ) ;
#116322=VECTOR ( 'NONE', #93269, 1000.000000000000000 ) ;
#116323=EDGE_CURVE ( 'NONE', #126742, #137862, #110138, .T. ) ;
#116324=CARTESIAN_POINT ( 'NONE',  ( 63.48921356237309510, -27.52281430457099631, 5.000000000000000000 ) ) ;
#116325=EDGE_LOOP ( 'NONE', ( #108647, #124619, #34418, #118310 ) ) ;
#116326=EDGE_CURVE ( 'NONE', #71721, #51167, #10817, .T. ) ;
#116327=ORIENTED_EDGE ( 'NONE', *, *, #117266, .T. ) ;
#116328=DIRECTION ( 'NONE',  ( 1.000000000000000000, 0.000000000000000000, 0.000000000000000000 ) ) ;
#116329=VERTEX_POINT ( 'NONE', #98563 ) ;
#116331=DIRECTION ( 'NONE',  ( 0.7071067811865487940, 0.7071067811865463515, -0.000000000000000000 ) ) ;
#116332=VECTOR ( 'NONE', #130786, 1000.000000000000000 ) ;
#116333=ADVANCED_FACE ( 'NONE', ( #142789 ), #43481, .F. ) ;
#116334=FACE_BOUND ( 'NONE', #137423, .T. ) ;
#116336=DIRECTION ( 'NONE',  ( 0.7071067811865487940, 0.7071067811865463515, 0.000000000000000000 ) ) ;
#116337=AXIS2_PLACEMENT_3D ( 'NONE', #38553, #63197, #63888 ) ;
#116338=DIRECTION ( 'NONE',  ( 0.7071067811865487940, 0.7071067811865463515, -0.000000000000000000 ) ) ;
#116339=VERTEX_POINT ( 'NONE', #75404 ) ;
#116340=EDGE_CURVE ( 'NONE', #94995, #39996, #119577, .T. ) ;
#116341=CARTESIAN_POINT ( 'NONE',  ( 17.20710678118642889, -17.24070752338410983, 5.000000000000000000 ) ) ;
#116344=ORIENTED_EDGE ( 'NONE', *, *, #9925, .T. ) ;
#116346=EDGE_LOOP ( 'NONE', ( #81874, #97660, #134472, #107917 ) ) ;
#116347=CARTESIAN_POINT ( 'NONE',  ( 20.20666063542138247, 21.75929247661549581, 4.998822639870702744 ) ) ;
#116348=DIRECTION ( 'NONE',  ( 0.7071067811865486830, -0.7071067811865464625, -0.000000000000000000 ) ) ;
#116349=VECTOR ( 'NONE', #28175, 1000.000000000000000 ) ;
#116350=AXIS2_PLACEMENT_3D ( 'NONE', #99445, #10999, #119765 ) ;
#116351=AXIS2_PLACEMENT_3D ( 'NONE', #74264, #92591, #137559 ) ;
#116352=VECTOR ( 'NONE', #11889, 1000.000000000000000 ) ;
#116354=LINE ( 'NONE', #49702, #72586 ) ;
#116355=ADVANCED_FACE ( 'NONE', ( #32620 ), #7966, .T. ) ;
#116358=CARTESIAN_POINT ( 'NONE',  ( 8.816011393731004731, 28.73617430169781173, 5.000000000000000000 ) ) ;
#116359=CARTESIAN_POINT ( 'NONE',  ( 2.510786437626908008, -27.52281430457053446, 5.000000000000000000 ) ) ;
#116361=CARTESIAN_POINT ( 'NONE',  ( -7.499999999999947597, -15.29013452822855257, 0.3645803511610184455 ) ) ;
#116362=EDGE_CURVE ( 'NONE', #100660, #97392, #52207, .T. ) ;
#116363=CARTESIAN_POINT ( 'NONE',  ( -13.08100000000000307, 3.174999999999997158, 1.444000000000000394 ) ) ;
#116364=DIRECTION ( 'NONE',  ( 0.6830127018922181881, 0.6830127018922202975, -0.2588190451025214056 ) ) ;
#116366=VECTOR ( 'NONE', #120909, 1000.000000000000000 ) ;
#116367=LINE ( 'NONE', #37384, #33025 ) ;
#116368=ORIENTED_EDGE ( 'NONE', *, *, #95013, .F. ) ;
#116369=DIRECTION ( 'NONE',  ( -0.000000000000000000, -0.3543493200069152693, 0.9351131265310292928 ) ) ;
#116371=CARTESIAN_POINT ( 'NONE',  ( -26.99999999999980460, 11.58746187583912324, 4.000000000000000000 ) ) ;
#116372=EDGE_LOOP ( 'NONE', ( #78564, #142638, #105611, #141714 ) ) ;
#116373=EDGE_LOOP ( 'NONE', ( #49334, #67549, #21892 ) ) ;
#116374=VERTEX_POINT ( 'NONE', #85528 ) ;
#116376=ORIENTED_EDGE ( 'NONE', *, *, #67747, .T. ) ;
#116379=ORIENTED_EDGE ( 'NONE', *, *, #90380, .F. ) ;
#116380=EDGE_CURVE ( 'NONE', #2022, #31707, #129764, .T. ) ;
#116381=LINE ( 'NONE', #84489, #43379 ) ;
#116383=CARTESIAN_POINT ( 'NONE',  ( -0.3281693992235228396, 17.25929247661554200, 4.000000000000000000 ) ) ;
#116384=CARTESIAN_POINT ( 'NONE',  ( -30.18398860626900060, 28.73617430169808173, 5.000000000000000000 ) ) ;
#116385=CARTESIAN_POINT ( 'NONE',  ( -45.18398860626900415, 28.73617430169818832, 5.000000000000000000 ) ) ;
#116386=ORIENTED_EDGE ( 'NONE', *, *, #136352, .T. ) ;
#116387=ORIENTED_EDGE ( 'NONE', *, *, #135745, .F. ) ;
#116388=CARTESIAN_POINT ( 'NONE',  ( 10.49999999999993605, 10.08746187583913922, 4.000000000000000000 ) ) ;
#116389=VECTOR ( 'NONE', #106527, 999.9999999999998863 ) ;
#116390=PLANE ( 'NONE',  #25351 ) ;
#116391=ORIENTED_EDGE ( 'NONE', *, *, #85453, .T. ) ;
#116392=LINE ( 'NONE', #51147, #45832 ) ;
#116393=EDGE_LOOP ( 'NONE', ( #84335, #36967, #78759, #140609 ) ) ;
#116395=ORIENTED_EDGE ( 'NONE', *, *, #52486, .T. ) ;
#116396=EDGE_CURVE ( 'NONE', #488, #38295, #19576, .T. ) ;
#116397=VECTOR ( 'NONE', #75766, 1000.000000000000000 ) ;
#116398=ORIENTED_EDGE ( 'NONE', *, *, #30537, .T. ) ;
#116399=ORIENTED_EDGE ( 'NONE', *, *, #82483, .T. ) ;
#116400=DIRECTION ( 'NONE',  ( 0.7071067811865487940, 0.7071067811865463515, -0.000000000000000000 ) ) ;
#116401=AXIS2_PLACEMENT_3D ( 'NONE', #38742, #129295, #140201 ) ;
#116402=AXIS2_PLACEMENT_3D ( 'NONE', #4085, #82435, #92562 ) ;
#116403=CARTESIAN_POINT ( 'NONE',  ( -31.49999999999977973, 0.4311230773921780335, 4.000000000000000000 ) ) ;
#116404=CARTESIAN_POINT ( 'NONE',  ( -32.29289321881322650, 17.25929247661554200, 5.000000000000000000 ) ) ;
#116405=EDGE_CURVE ( 'NONE', #9952, #13889, #51269, .T. ) ;
#116406=LINE ( 'NONE', #138164, #90279 ) ;
#116407=ORIENTED_EDGE ( 'NONE', *, *, #107653, .T. ) ;
#116408=CARTESIAN_POINT ( 'NONE',  ( 1.171830600776462061, -2.240707523384260824, 4.000000000000000000 ) ) ;
#116409=EDGE_CURVE ( 'NONE', #18530, #99520, #63595, .T. ) ;
#116410=VERTEX_POINT ( 'NONE', #6986 ) ;
#116411=LINE ( 'NONE', #139626, #95703 ) ;
#116414=EDGE_CURVE ( 'NONE', #95607, #54775, #96157, .T. ) ;
#116415=CARTESIAN_POINT ( 'NONE',  ( 8.207106781186491062, 6.759292476615645917, 5.000000000000000000 ) ) ;
#116416=LINE ( 'NONE', #127276, #129402 ) ;
#116418=ORIENTED_EDGE ( 'NONE', *, *, #118996, .F. ) ;
#116419=VERTEX_POINT ( 'NONE', #107754 ) ;
#116420=VECTOR ( 'NONE', #58258, 999.9999999999998863 ) ;
#116421=ORIENTED_EDGE ( 'NONE', *, *, #5312, .F. ) ;
#116422=CARTESIAN_POINT ( 'NONE',  ( 0.000000000000000000, 0.000000000000000000, 5.000000000000000000 ) ) ;
#116423=LINE ( 'NONE', #126559, #85945 ) ;
#116425=AXIS2_PLACEMENT_3D ( 'NONE', #26777, #39088, #49284 ) ;
#116426=LINE ( 'NONE', #17112, #19627 ) ;
#116431=CARTESIAN_POINT ( 'NONE',  ( 1.499999999999991784, -16.91253812416058722, 4.000000000000000000 ) ) ;
#116433=DIRECTION ( 'NONE',  ( -0.7071067811865487940, 0.7071067811865463515, 0.000000000000000000 ) ) ;
#116434=CARTESIAN_POINT ( 'NONE',  ( -30.18398860626900060, 28.73617430169808173, 5.000000000000000000 ) ) ;
#116435=CARTESIAN_POINT ( 'NONE',  ( 34.49999999999975131, 13.08746187583911436, 4.000000000000000000 ) ) ;
#116436=EDGE_LOOP ( 'NONE', ( #87960, #7195, #59975, #37211 ) ) ;
#116437=VECTOR ( 'NONE', #119493, 999.9999999999998863 ) ;
#116438=DIRECTION ( 'NONE',  ( -0.000000000000000000, 0.3543493200069153248, 0.9351131265310292928 ) ) ;
#116440=LINE ( 'NONE', #41018, #2124 ) ;
#116441=CARTESIAN_POINT ( 'NONE',  ( 11.67183060077639212, 11.25929247661560240, 4.000000000000000000 ) ) ;
#116442=ORIENTED_EDGE ( 'NONE', *, *, #73214, .T. ) ;
#116443=EDGE_CURVE ( 'NONE', #27577, #74390, #82465, .T. ) ;
#116444=DIRECTION ( 'NONE',  ( 0.7071067811865487940, -0.7071067811865463515, 0.000000000000000000 ) ) ;
#116446=ORIENTED_EDGE ( 'NONE', *, *, #123469, .T. ) ;
#116447=AXIS2_PLACEMENT_3D ( 'NONE', #78882, #135408, #81015 ) ;
#116448=ORIENTED_EDGE ( 'NONE', *, *, #124711, .T. ) ;
#116449=CARTESIAN_POINT ( 'NONE',  ( 9.707106781186476852, -12.74070752338415247, 5.000000000000000000 ) ) ;
#116450=DIRECTION ( 'NONE',  ( 0.7071067811865487940, 0.7071067811865463515, -0.000000000000000000 ) ) ;
#116452=LINE ( 'NONE', #3374, #113467 ) ;
#116455=DIRECTION ( 'NONE',  ( -0.7071067811865486830, -0.7071067811865464625, 0.000000000000000000 ) ) ;
#116457=CARTESIAN_POINT ( 'NONE',  ( 34.82816939922328459, 9.759292476615618384, 4.000000000000000000 ) ) ;
#116458=VECTOR ( 'NONE', #108711, 1000.000000000000000 ) ;
#116459=LINE ( 'NONE', #73673, #60676 ) ;
#116460=ORIENTED_EDGE ( 'NONE', *, *, #17645, .T. ) ;
#116462=VECTOR ( 'NONE', #35813, 1000.000000000000227 ) ;
#116464=VERTEX_POINT ( 'NONE', #49853 ) ;
#116466=CARTESIAN_POINT ( 'NONE',  ( -14.51078643762690490, -27.52281430457045275, 5.000000000000000000 ) ) ;
#116467=EDGE_CURVE ( 'NONE', #50272, #103277, #95463, .T. ) ;
#116468=AXIS2_PLACEMENT_3D ( 'NONE', #3087, #80674, #48048 ) ;
#116469=LINE ( 'NONE', #6227, #127980 ) ;
#116471=CARTESIAN_POINT ( 'NONE',  ( 5.816011393731002066, 28.73617430169783304, 5.000000000000000000 ) ) ;
#116472=VERTEX_POINT ( 'NONE', #107055 ) ;
#116473=CARTESIAN_POINT ( 'NONE',  ( 11.99999999999992006, 20.96639925780204905, 5.000000000000000000 ) ) ;
#116474=CARTESIAN_POINT ( 'NONE',  ( -34.92500000000001137, -22.22500000000000142, 4.000000000000000000 ) ) ;
#116475=CARTESIAN_POINT ( 'NONE',  ( -42.18398860626899705, 28.73617430169816700, 5.000000000000000000 ) ) ;
#116476=DIRECTION ( 'NONE',  ( -0.6830127018922180770, -0.6830127018922204085, -0.2588190451025213501 ) ) ;
#116477=EDGE_LOOP ( 'NONE', ( #18883, #134153, #63478, #48701 ) ) ;
#116479=CARTESIAN_POINT ( 'NONE',  ( -34.92500000000001137, 2.718490437204206689, 4.759050581649335143 ) ) ;
#116481=LINE ( 'NONE', #28774, #40064 ) ;
#116482=EDGE_LOOP ( 'NONE', ( #130307, #36431, #115016 ) ) ;
#116483=ORIENTED_EDGE ( 'NONE', *, *, #69567, .F. ) ;
#116484=EDGE_CURVE ( 'NONE', #48744, #41026, #71591, .T. ) ;
#116486=AXIS2_PLACEMENT_3D ( 'NONE', #131418, #33557, #99462 ) ;
#116487=ORIENTED_EDGE ( 'NONE', *, *, #88666, .F. ) ;
#116488=EDGE_CURVE ( 'NONE', #72213, #77576, #29482, .T. ) ;
#116490=EDGE_CURVE ( 'NONE', #15277, #57196, #98290, .T. ) ;
#116491=FACE_OUTER_BOUND ( 'NONE', #104403, .T. ) ;
#116492=CARTESIAN_POINT ( 'NONE',  ( -54.18398860626899705, 28.73617430169825226, 5.000000000000000000 ) ) ;
#116493=VERTEX_POINT ( 'NONE', #83923 ) ;
#116494=EDGE_CURVE ( 'NONE', #88587, #52361, #128118, .T. ) ;
#116495=LINE ( 'NONE', #6252, #109379 ) ;
#116496=CARTESIAN_POINT ( 'NONE',  ( -1.499999999999987566, 9.052185695429084689, 5.000000000000000000 ) ) ;
#116498=ORIENTED_EDGE ( 'NONE', *, *, #110385, .F. ) ;
#116499=VECTOR ( 'NONE', #33689, 999.9999999999998863 ) ;
#116501=CARTESIAN_POINT ( 'NONE',  ( -0.1839886062690032631, 28.73617430169787568, 5.000000000000000000 ) ) ;
#116502=CARTESIAN_POINT ( 'NONE',  ( -25.49999999999982236, -19.53360074219753884, 5.000000000000000000 ) ) ;
#116503=DIRECTION ( 'NONE',  ( 0.7071067811865487940, 0.7071067811865463515, -0.000000000000000000 ) ) ;
#116505=ORIENTED_EDGE ( 'NONE', *, *, #134051, .T. ) ;
#116506=VECTOR ( 'NONE', #57769, 1000.000000000000000 ) ;
#116507=ORIENTED_EDGE ( 'NONE', *, *, #59968, .T. ) ;
#116508=EDGE_CURVE ( 'NONE', #26469, #1535, #139198, .T. ) ;
#116509=EDGE_CURVE ( 'NONE', #48269, #41471, #37737, .T. ) ;
#116510=LINE ( 'NONE', #17197, #29228 ) ;
#116511=FACE_OUTER_BOUND ( 'NONE', #54915, .T. ) ;
#116513=CARTESIAN_POINT ( 'NONE',  ( -17.70025512860841488, -27.71228299555193786, 4.000000000000000000 ) ) ;
#116514=EDGE_CURVE ( 'NONE', #39920, #88187, #127584, .T. ) ;
#116515=VECTOR ( 'NONE', #96866, 999.9999999999998863 ) ;
#116516=FACE_OUTER_BOUND ( 'NONE', #127617, .T. ) ;
#116517=ORIENTED_EDGE ( 'NONE', *, *, #102975, .F. ) ;
#116518=VECTOR ( 'NONE', #60648, 999.9999999999998863 ) ;
#116519=VERTEX_POINT ( 'NONE', #62346 ) ;
#116521=VERTEX_POINT ( 'NONE', #73219 ) ;
#116522=AXIS2_PLACEMENT_3D ( 'NONE', #23502, #69172, #89474 ) ;
#116526=CARTESIAN_POINT ( 'NONE',  ( -2.510786437626908008, -27.52281430457053446, 5.000000000000000000 ) ) ;
#116527=DIRECTION ( 'NONE',  ( -0.000000000000000000, 0.3543493200069153248, 0.9351131265310292928 ) ) ;
#116528=CARTESIAN_POINT ( 'NONE',  ( 34.49999999999975842, -7.535744391599426883, 4.994342998332164107 ) ) ;
#116529=EDGE_CURVE ( 'NONE', #77399, #140629, #28843, .T. ) ;
#116530=DIRECTION ( 'NONE',  ( -0.000000000000000000, 0.3543493200069153248, 0.9351131265310292928 ) ) ;
#116531=AXIS2_PLACEMENT_3D ( 'NONE', #47560, #15544, #125797 ) ;
#116532=DIRECTION ( 'NONE',  ( -0.7071067811865487940, 0.7071067811865463515, 0.000000000000000000 ) ) ;
#116533=EDGE_LOOP ( 'NONE', ( #61797, #123907, #100576, #127625 ) ) ;
#116534=CARTESIAN_POINT ( 'NONE',  ( -21.79333936457831911, 21.75929247661549226, 4.998822639870701856 ) ) ;
#116535=DIRECTION ( 'NONE',  ( 0.7071067811865487940, 0.7071067811865463515, 0.000000000000000000 ) ) ;
#116536=ORIENTED_EDGE ( 'NONE', *, *, #130455, .T. ) ;
#116537=DIRECTION ( 'NONE',  ( 0.6830127018922181881, 0.6830127018922202975, -0.2588190451025214056 ) ) ;
#116538=EDGE_LOOP ( 'NONE', ( #87675, #1698, #3857, #98524 ) ) ;
#116539=VERTEX_POINT ( 'NONE', #103650 ) ;
#116541=EDGE_LOOP ( 'NONE', ( #135711, #85088, #32371, #37572, #1007 ) ) ;
#116542=ORIENTED_EDGE ( 'NONE', *, *, #85247, .F. ) ;
#116543=AXIS2_PLACEMENT_3D ( 'NONE', #112042, #2519, #44679 ) ;
#116545=VERTEX_POINT ( 'NONE', #70399 ) ;
#116546=EDGE_CURVE ( 'NONE', #42161, #98060, #5769, .T. ) ;
#116547=CARTESIAN_POINT ( 'NONE',  ( -31.49999999999977973, -14.56887692260766087, 4.000000000000000000 ) ) ;
#116548=VECTOR ( 'NONE', #22909, 999.9999999999998863 ) ;
#116549=CARTESIAN_POINT ( 'NONE',  ( -69.18398860626899705, 28.73617430169835529, 5.000000000000000000 ) ) ;
#116551=CARTESIAN_POINT ( 'NONE',  ( -39.48921356237310221, -27.52281430457082934, 5.000000000000000000 ) ) ;
#116552=EDGE_CURVE ( 'NONE', #113440, #20682, #18057, .T. ) ;
#116553=DIRECTION ( 'NONE',  ( 0.6830127018922180770, -0.6830127018922204085, -0.2588190451025213501 ) ) ;
#116554=CARTESIAN_POINT ( 'NONE',  ( -24.48921356237309510, -27.52281430457072631, 5.000000000000000000 ) ) ;
#116555=DIRECTION ( 'NONE',  ( -0.7071067811865486830, -0.7071067811865464625, 0.000000000000000000 ) ) ;
#116556=VECTOR ( 'NONE', #129737, 999.9999999999998863 ) ;
#116559=VERTEX_POINT ( 'NONE', #104382 ) ;
#116560=ADVANCED_FACE ( 'NONE', ( #136305 ), #7187, .F. ) ;
#116561=ORIENTED_EDGE ( 'NONE', *, *, #128984, .T. ) ;
#116562=VERTEX_POINT ( 'NONE', #84112 ) ;
#116563=VECTOR ( 'NONE', #84765, 999.9999999999998863 ) ;
#116564=PLANE ( 'NONE',  #25564 ) ;
#116565=FACE_OUTER_BOUND ( 'NONE', #133773, .T. ) ;
#116566=ORIENTED_EDGE ( 'NONE', *, *, #37440, .F. ) ;
#116567=LINE ( 'NONE', #105662, #46920 ) ;
#116568=DIRECTION ( 'NONE',  ( -0.3543493200069162685, -0.000000000000000000, -0.9351131265310288487 ) ) ;
#116569=EDGE_CURVE ( 'NONE', #112632, #59289, #138466, .T. ) ;
#116570=DIRECTION ( 'NONE',  ( -0.000000000000000000, 0.000000000000000000, 1.000000000000000000 ) ) ;
#116571=LINE ( 'NONE', #83235, #50982 ) ;
#116572=ORIENTED_EDGE ( 'NONE', *, *, #102741, .F. ) ;
#116574=EDGE_LOOP ( 'NONE', ( #108032, #30131, #57330 ) ) ;
#116576=VECTOR ( 'NONE', #121767, 1000.000000000000227 ) ;
#116578=CARTESIAN_POINT ( 'NONE',  ( -21.48921356237309155, -27.52281430457070499, 5.000000000000000000 ) ) ;
#116579=LINE ( 'NONE', #17263, #27354 ) ;
#116581=ORIENTED_EDGE ( 'NONE', *, *, #120662, .F. ) ;
#116582=ORIENTED_EDGE ( 'NONE', *, *, #89621, .F. ) ;
#116583=ORIENTED_EDGE ( 'NONE', *, *, #99922, .F. ) ;
#116584=CARTESIAN_POINT ( 'NONE',  ( -14.29289321881335972, 11.25929247661560240, 5.000000000000000000 ) ) ;
#116585=CARTESIAN_POINT ( 'NONE',  ( 0.000000000000000000, 0.000000000000000000, 5.000000000000000000 ) ) ;
#116587=FACE_OUTER_BOUND ( 'NONE', #134159, .T. ) ;
#116588=VECTOR ( 'NONE', #126367, 1000.000000000000000 ) ;
#116589=PLANE ( 'NONE',  #4240 ) ;
#116590=DIRECTION ( 'NONE',  ( 0.7071067811865487940, 0.7071067811865463515, -0.000000000000000000 ) ) ;
#116591=DIRECTION ( 'NONE',  ( 0.7071067811865486830, -0.7071067811865464625, -0.000000000000000000 ) ) ;
#116592=EDGE_CURVE ( 'NONE', #127118, #43460, #28278, .T. ) ;
#116594=DIRECTION ( 'NONE',  ( -0.7071067811865486830, 0.7071067811865464625, 0.000000000000000000 ) ) ;
#116595=LINE ( 'NONE', #62959, #21112 ) ;
#116597=LINE ( 'NONE', #17280, #81125 ) ;
#116598=LINE ( 'NONE', #17281, #105429 ) ;
#116599=ORIENTED_EDGE ( 'NONE', *, *, #50552, .F. ) ;
#116600=AXIS2_PLACEMENT_3D ( 'NONE', #6706, #49587, #38678 ) ;
#116601=PLANE ( 'NONE',  #8937 ) ;
#116602=EDGE_CURVE ( 'NONE', #90399, #119015, #72539, .T. ) ;
#116603=LINE ( 'NONE', #17964, #23313 ) ;
#116604=EDGE_LOOP ( 'NONE', ( #29395, #86103, #22177 ) ) ;
#116605=EDGE_CURVE ( 'NONE', #113212, #117294, #26133, .T. ) ;
#116606=DIRECTION ( 'NONE',  ( -0.7071067811865487940, 0.7071067811865463515, 0.000000000000000000 ) ) ;
#116609=PLANE ( 'NONE',  #97521 ) ;
#116611=VECTOR ( 'NONE', #96701, 1000.000000000000114 ) ;
#116612=LINE ( 'NONE', #126754, #73056 ) ;
#116614=DIRECTION ( 'NONE',  ( -0.6830127018922180770, -0.6830127018922204085, -0.2588190451025213501 ) ) ;
#116616=CARTESIAN_POINT ( 'NONE',  ( 34.75611968250419892, 17.81293425470720848, 4.955485411084877612 ) ) ;
#116617=DIRECTION ( 'NONE',  ( 0.7071067811865487940, 0.7071067811865463515, 0.000000000000000000 ) ) ;
#116618=DIRECTION ( 'NONE',  ( 0.6830127018922180770, -0.6830127018922204085, -0.2588190451025213501 ) ) ;
#116619=CARTESIAN_POINT ( 'NONE',  ( 41.99451991528749062, 28.92564299267967343, 4.000000000000000000 ) ) ;
#116622=AXIS2_PLACEMENT_3D ( 'NONE', #112658, #55434, #80765 ) ;
#116623=DIRECTION ( 'NONE',  ( -0.3543493200069162685, -0.000000000000000000, -0.9351131265310288487 ) ) ;
#116624=PLANE ( 'NONE',  #109157 ) ;
#116628=ORIENTED_EDGE ( 'NONE', *, *, #115687, .T. ) ;
#116630=CARTESIAN_POINT ( 'NONE',  ( 31.49999999999977973, -4.796895815300992183, -3.611700055028608247 ) ) ;
#116631=EDGE_LOOP ( 'NONE', ( #6691, #25272, #136189, #72706, #84165 ) ) ;
#116632=CARTESIAN_POINT ( 'NONE',  ( 20.29289321881331531, -3.740707523384241728, 5.000000000000000000 ) ) ;
#116635=VERTEX_POINT ( 'NONE', #116701 ) ;
#116636=DIRECTION ( 'NONE',  ( 0.3543493200069162685, -0.000000000000000000, -0.9351131265310288487 ) ) ;
#116637=CARTESIAN_POINT ( 'NONE',  ( 50.99451991528749062, 28.92564299267973738, 4.000000000000000000 ) ) ;
#116638=CARTESIAN_POINT ( 'NONE',  ( -26.81601139373100651, 28.73617430169768738, 5.000000000000000000 ) ) ;
#116639=DIRECTION ( 'NONE',  ( -0.6830127018922181881, 0.6830127018922202975, -0.2588190451025214056 ) ) ;
#116640=LINE ( 'NONE', #126110, #137343 ) ;
#116641=DIRECTION ( 'NONE',  ( -0.000000000000000000, 0.3543493200069153248, 0.9351131265310292928 ) ) ;
#116642=CARTESIAN_POINT ( 'NONE',  ( -33.48921356237309510, -27.52281430457078670, 5.000000000000000000 ) ) ;
#116643=FACE_OUTER_BOUND ( 'NONE', #91765, .T. ) ;
#116644=FACE_OUTER_BOUND ( 'NONE', #142107, .T. ) ;
#116647=EDGE_LOOP ( 'NONE', ( #137109, #44139, #52848, #82141 ) ) ;
#116648=EDGE_LOOP ( 'NONE', ( #75600, #142624, #35383, #138447 ) ) ;
#116649=EDGE_CURVE ( 'NONE', #57318, #115599, #137761, .T. ) ;
#116651=ORIENTED_EDGE ( 'NONE', *, *, #61710, .T. ) ;
#116652=EDGE_CURVE ( 'NONE', #37230, #137445, #39151, .T. ) ;
#116653=DIRECTION ( 'NONE',  ( -0.3543493200069163240, 0.000000000000000000, 0.9351131265310288487 ) ) ;
#116654=LINE ( 'NONE', #17341, #61992 ) ;
#116655=VERTEX_POINT ( 'NONE', #81972 ) ;
#116656=EDGE_CURVE ( 'NONE', #129709, #56655, #71080, .T. ) ;
#116657=EDGE_CURVE ( 'NONE', #70306, #36106, #102946, .T. ) ;
#116658=CARTESIAN_POINT ( 'NONE',  ( -20.93988928955967310, -9.740707523384180888, 10.89222023123385874 ) ) ;
#116659=PLANE ( 'NONE',  #48921 ) ;
#116662=ORIENTED_EDGE ( 'NONE', *, *, #109610, .T. ) ;
#116664=EDGE_LOOP ( 'NONE', ( #21210, #113449, #121555, #95816 ) ) ;
#116665=LINE ( 'NONE', #17350, #123944 ) ;
#116666=LINE ( 'NONE', #60915, #79336 ) ;
#116667=CARTESIAN_POINT ( 'NONE',  ( 17.81601139373099940, 28.73617430169775133, 5.000000000000000000 ) ) ;
#116668=CARTESIAN_POINT ( 'NONE',  ( 2.671830600776460063, 20.25929247661551713, 4.000000000000000000 ) ) ;
#116669=ORIENTED_EDGE ( 'NONE', *, *, #108935, .F. ) ;
#116670=ORIENTED_EDGE ( 'NONE', *, *, #111996, .F. ) ;
#116671=EDGE_CURVE ( 'NONE', #99825, #83817, #15911, .T. ) ;
#116672=ORIENTED_EDGE ( 'NONE', *, *, #15290, .F. ) ;
#116673=LINE ( 'NONE', #94196, #130134 ) ;
#116675=DIRECTION ( 'NONE',  ( -0.6830127018922181881, 0.6830127018922202975, -0.2588190451025214056 ) ) ;
#116677=VECTOR ( 'NONE', #85873, 1000.000000000000227 ) ;
#116678=DIRECTION ( 'NONE',  ( -0.000000000000000000, -0.3543493200069152693, 0.9351131265310292928 ) ) ;
#116679=EDGE_CURVE ( 'NONE', #51279, #86186, #40587, .T. ) ;
#116681=VECTOR ( 'NONE', #13909, 999.9999999999998863 ) ;
#116682=ORIENTED_EDGE ( 'NONE', *, *, #128443, .F. ) ;
#116683=ORIENTED_EDGE ( 'NONE', *, *, #25732, .F. ) ;
#116684=DIRECTION ( 'NONE',  ( 0.7071067811865487940, 0.7071067811865463515, -0.000000000000000000 ) ) ;
#116685=ORIENTED_EDGE ( 'NONE', *, *, #142409, .F. ) ;
#116686=ORIENTED_EDGE ( 'NONE', *, *, #127973, .F. ) ;
#116689=CARTESIAN_POINT ( 'NONE',  ( -26.99999999999980815, -16.02097659208073566, -11.96015758381202154 ) ) ;
#116690=DIRECTION ( 'NONE',  ( 0.7071067811865487940, 0.7071067811865463515, -0.000000000000000000 ) ) ;
#116691=ORIENTED_EDGE ( 'NONE', *, *, #13560, .T. ) ;
#116693=CARTESIAN_POINT ( 'NONE',  ( 48.48921356237309510, -27.52281430457089328, 5.000000000000000000 ) ) ;
#116695=CARTESIAN_POINT ( 'NONE',  ( 14.99999999999990230, 14.96639925780210767, 5.000000000000000000 ) ) ;
#116696=EDGE_CURVE ( 'NONE', #21017, #11525, #9321, .T. ) ;
#116697=CARTESIAN_POINT ( 'NONE',  ( 24.29974487139158867, -27.71228299555223273, 4.000000000000000000 ) ) ;
#116698=CARTESIAN_POINT ( 'NONE',  ( -29.99999999999979394, 10.93112307739207623, 4.000000000000000000 ) ) ;
#116699=ORIENTED_EDGE ( 'NONE', *, *, #19765, .T. ) ;
#116701=CARTESIAN_POINT ( 'NONE',  ( 26.99999999999980815, -12.03360074219761700, 5.000000000000000000 ) ) ;
#116703=AXIS2_PLACEMENT_3D ( 'NONE', #9563, #141544, #96561 ) ;
#116704=ORIENTED_EDGE ( 'NONE', *, *, #54819, .F. ) ;
#116705=PLANE ( 'NONE',  #110544 ) ;
#116706=PLANE ( 'NONE',  #59706 ) ;
#116708=VERTEX_POINT ( 'NONE', #32565 ) ;
#116710=LINE ( 'NONE', #128320, #119978 ) ;
#116711=VERTEX_POINT ( 'NONE', #65208 ) ;
#116712=EDGE_CURVE ( 'NONE', #5308, #25358, #139909, .T. ) ;
#116714=ORIENTED_EDGE ( 'NONE', *, *, #39170, .F. ) ;
#116715=EDGE_CURVE ( 'NONE', #130843, #41370, #54340, .T. ) ;
#116719=DIRECTION ( 'NONE',  ( 0.7071067811865487940, 0.7071067811865463515, 0.000000000000000000 ) ) ;
#116720=LINE ( 'NONE', #117402, #63462 ) ;
#116721=LINE ( 'NONE', #26848, #18333 ) ;
#116722=DIRECTION ( 'NONE',  ( 0.7071067811865487940, 0.7071067811865463515, 0.000000000000000000 ) ) ;
#116723=DIRECTION ( 'NONE',  ( 0.7071067811865486830, -0.7071067811865464625, -0.000000000000000000 ) ) ;
#116724=LINE ( 'NONE', #17402, #134946 ) ;
#116728=CARTESIAN_POINT ( 'NONE',  ( -35.99451991528749772, 28.92564299267963079, 4.000000000000000000 ) ) ;
#116729=EDGE_CURVE ( 'NONE', #55828, #110463, #43431, .T. ) ;
#116731=ORIENTED_EDGE ( 'NONE', *, *, #64806, .T. ) ;
#116732=AXIS2_PLACEMENT_3D ( 'NONE', #81858, #135504, #70962 ) ;
#116733=ORIENTED_EDGE ( 'NONE', *, *, #79210, .T. ) ;
#116734=ORIENTED_EDGE ( 'NONE', *, *, #2699, .F. ) ;
#116735=DIRECTION ( 'NONE',  ( -0.7071067811865486830, 0.7071067811865464625, 0.000000000000000000 ) ) ;
#116736=ORIENTED_EDGE ( 'NONE', *, *, #57932, .T. ) ;
#116737=ORIENTED_EDGE ( 'NONE', *, *, #43906, .T. ) ;
#116738=DIRECTION ( 'NONE',  ( 0.6830127018922180770, -0.6830127018922204085, -0.2588190451025213501 ) ) ;
#116739=CARTESIAN_POINT ( 'NONE',  ( -3.183988606268992161, 28.73617430169789699, 5.000000000000000000 ) ) ;
#116740=ORIENTED_EDGE ( 'NONE', *, *, #54102, .T. ) ;
#116741=LINE ( 'NONE', #118137, #30228 ) ;
#116742=ORIENTED_EDGE ( 'NONE', *, *, #142344, .T. ) ;
#116743=CARTESIAN_POINT ( 'NONE',  ( -29.99999999999979039, -18.03360074219754949, 5.000000000000000000 ) ) ;
#116744=LINE ( 'NONE', #92122, #86725 ) ;
#116746=ORIENTED_EDGE ( 'NONE', *, *, #72179, .T. ) ;
#116748=CARTESIAN_POINT ( 'NONE',  ( -8.207106781186485733, -2.240707523384259492, 5.000000000000000000 ) ) ;
#116749=FACE_OUTER_BOUND ( 'NONE', #123805, .T. ) ;
#116750=VERTEX_POINT ( 'NONE', #20945 ) ;
#116751=ORIENTED_EDGE ( 'NONE', *, *, #112105, .F. ) ;
#116752=( LENGTH_UNIT ( ) NAMED_UNIT ( * ) SI_UNIT ( .MILLI., .METRE. ) );
#116753=VERTEX_POINT ( 'NONE', #109393 ) ;
#116755=DIRECTION ( 'NONE',  ( 0.7071067811865486830, -0.7071067811865464625, -0.000000000000000000 ) ) ;
#116756=DIRECTION ( 'NONE',  ( 0.6830127018922181881, 0.6830127018922202975, -0.2588190451025214056 ) ) ;
#116758=VECTOR ( 'NONE', #21140, 1000.000000000000000 ) ;
#116759=VERTEX_POINT ( 'NONE', #20217 ) ;
#116760=LINE ( 'NONE', #61700, #46031 ) ;
#116761=EDGE_CURVE ( 'NONE', #14518, #39863, #128996, .T. ) ;
#116762=CARTESIAN_POINT ( 'NONE',  ( -17.29289321881333308, 11.25929247661560240, 5.000000000000000000 ) ) ;
#116765=FACE_OUTER_BOUND ( 'NONE', #49745, .T. ) ;
#116766=DIRECTION ( 'NONE',  ( -0.6830127018922181881, 0.6830127018922202975, -0.2588190451025214056 ) ) ;
#116767=ORIENTED_EDGE ( 'NONE', *, *, #94025, .T. ) ;
#116768=EDGE_CURVE ( 'NONE', #22223, #108166, #30414, .T. ) ;
#116771=EDGE_CURVE ( 'NONE', #141085, #74995, #18801, .T. ) ;
#116772=VERTEX_POINT ( 'NONE', #52157 ) ;
#116774=CARTESIAN_POINT ( 'NONE',  ( -51.18398860626899705, 28.73617430169823095, 5.000000000000000000 ) ) ;
#116775=AXIS2_PLACEMENT_3D ( 'NONE', #120430, #121176, #65416 ) ;
#116776=ORIENTED_EDGE ( 'NONE', *, *, #31396, .F. ) ;
#116777=DIRECTION ( 'NONE',  ( -0.7071067811865486830, -0.7071067811865464625, -0.000000000000000000 ) ) ;
#116778=VECTOR ( 'NONE', #115177, 1000.000000000000000 ) ;
#116780=VERTEX_POINT ( 'NONE', #96336 ) ;
#116781=EDGE_CURVE ( 'NONE', #8977, #116077, #74649, .T. ) ;
#116782=FACE_OUTER_BOUND ( 'NONE', #132271, .T. ) ;
#116783=VECTOR ( 'NONE', #27114, 1000.000000000000227 ) ;
#116784=FACE_OUTER_BOUND ( 'NONE', #50629, .T. ) ;
#116785=CARTESIAN_POINT ( 'NONE',  ( 18.99507522778794666, -5.240707523384225297, 12.38332538355491508 ) ) ;
#116786=DIRECTION ( 'NONE',  ( 0.6830127018922180770, -0.6830127018922204085, -0.2588190451025213501 ) ) ;
#116787=CARTESIAN_POINT ( 'NONE',  ( 21.48921356237309155, -27.52281430457070499, 5.000000000000000000 ) ) ;
#116788=CARTESIAN_POINT ( 'NONE',  ( 27.48921356237309155, -27.52281430457074762, 5.000000000000000000 ) ) ;
#116789=LINE ( 'NONE', #37832, #76168 ) ;
#116790=LINE ( 'NONE', #118929, #81243 ) ;
#116791=CARTESIAN_POINT ( 'NONE',  ( 7.499999999999958256, 4.087461875839200509, 4.000000000000000000 ) ) ;
#116792=ORIENTED_EDGE ( 'NONE', *, *, #123890, .F. ) ;
#116794=VERTEX_POINT ( 'NONE', #113672 ) ;
#116795=VERTEX_POINT ( 'NONE', #99953 ) ;
#116797=ORIENTED_EDGE ( 'NONE', *, *, #26794, .F. ) ;
#116798=VECTOR ( 'NONE', #2074, 1000.000000000000000 ) ;
#116799=ORIENTED_EDGE ( 'NONE', *, *, #140971, .F. ) ;
#116800=ORIENTED_EDGE ( 'NONE', *, *, #119030, .F. ) ;
#116802=CARTESIAN_POINT ( 'NONE',  ( 20.29289321881331887, 17.25929247661554911, 5.000000000000000000 ) ) ;
#116803=ADVANCED_FACE ( 'NONE', ( #25232 ), #69488, .T. ) ;
#116804=VERTEX_POINT ( 'NONE', #123151 ) ;
#116806=CARTESIAN_POINT ( 'NONE',  ( -14.81601139373099585, 28.73617430169776910, 5.000000000000000000 ) ) ;
#116808=FACE_OUTER_BOUND ( 'NONE', #40763, .T. ) ;
#116810=VERTEX_POINT ( 'NONE', #110791 ) ;
#116811=FACE_OUTER_BOUND ( 'NONE', #2194, .T. ) ;
#116812=CARTESIAN_POINT ( 'NONE',  ( 33.29177708983026918, -15.74070752338412049, 19.73771281079105222 ) ) ;
#116813=PLANE ( 'NONE',  #77494 ) ;
#116814=CARTESIAN_POINT ( 'NONE',  ( -28.49999999999980105, -2.173586137069166924, -4.605770156576174834 ) ) ;
#116817=DIRECTION ( 'NONE',  ( -0.3543493200069162685, -0.000000000000000000, -0.9351131265310288487 ) ) ;
#116820=CARTESIAN_POINT ( 'NONE',  ( -15.48921356237309510, -27.52281430457066236, 5.000000000000000000 ) ) ;
#116821=VECTOR ( 'NONE', #40124, 1000.000000000000227 ) ;
#116822=DIRECTION ( 'NONE',  ( 0.7071067811865487940, 0.7071067811865463515, 0.000000000000000000 ) ) ;
#116823=ORIENTED_EDGE ( 'NONE', *, *, #34314, .F. ) ;
#116825=VECTOR ( 'NONE', #142111, 1000.000000000000000 ) ;
#116827=ORIENTED_EDGE ( 'NONE', *, *, #65769, .T. ) ;
#116829=CARTESIAN_POINT ( 'NONE',  ( -17.81601139373099940, 28.73617430169775133, 5.000000000000000000 ) ) ;
#116830=EDGE_CURVE ( 'NONE', #65419, #91252, #80366, .T. ) ;
#116831=FACE_OUTER_BOUND ( 'NONE', #92834, .T. ) ;
#116832=DIRECTION ( 'NONE',  ( -0.3543493200069163240, -0.000000000000000000, -0.9351131265310288487 ) ) ;
#116833=CARTESIAN_POINT ( 'NONE',  ( -19.05000000000000071, 3.174999999999997158, 0.000000000000000000 ) ) ;
#116834=EDGE_CURVE ( 'NONE', #62799, #24662, #66619, .T. ) ;
#116836=CARTESIAN_POINT ( 'NONE',  ( 19.05000000000000071, 3.174999999999997158, 1.444000000000000394 ) ) ;
#116838=ORIENTED_EDGE ( 'NONE', *, *, #620, .T. ) ;
#116840=VERTEX_POINT ( 'NONE', #124557 ) ;
#116842=EDGE_CURVE ( 'NONE', #60629, #47758, #57194, .T. ) ;
#116844=DIRECTION ( 'NONE',  ( 0.7071067811865486830, -0.7071067811865464625, -0.000000000000000000 ) ) ;
#116846=ORIENTED_EDGE ( 'NONE', *, *, #140884, .T. ) ;
#116848=EDGE_CURVE ( 'NONE', #73530, #109556, #12918, .T. ) ;
#116849=ORIENTED_EDGE ( 'NONE', *, *, #54815, .F. ) ;
#116850=FACE_OUTER_BOUND ( 'NONE', #45841, .T. ) ;
#116851=EDGE_CURVE ( 'NONE', #123173, #46980, #143440, .T. ) ;
#116852=CARTESIAN_POINT ( 'NONE',  ( -7.637538124160930586, 22.22500000000000142, 4.000000000000000000 ) ) ;
#116853=CARTESIAN_POINT ( 'NONE',  ( 19.05000000000000071, 3.174999999999997158, 5.000000000000000000 ) ) ;
#116854=DIRECTION ( 'NONE',  ( -0.7071067811865487940, 0.7071067811865463515, -0.000000000000000000 ) ) ;
#116855=EDGE_CURVE ( 'NONE', #133448, #98744, #2013, .T. ) ;
#116856=ADVANCED_FACE ( 'NONE', ( #11474 ), #44157, .F. ) ;
#116858=ORIENTED_EDGE ( 'NONE', *, *, #54228, .F. ) ;
#116859=LINE ( 'NONE', #17536, #55855 ) ;
#116861=EDGE_LOOP ( 'NONE', ( #46269, #25910, #135113 ) ) ;
#116862=VERTEX_POINT ( 'NONE', #24522 ) ;
#116863=PLANE ( 'NONE',  #137231 ) ;
#116864=EDGE_CURVE ( 'NONE', #36373, #107048, #132618, .T. ) ;
#116865=ORIENTED_EDGE ( 'NONE', *, *, #64349, .T. ) ;
#116866=AXIS2_PLACEMENT_3D ( 'NONE', #632, #65225, #76076 ) ;
#116867=CARTESIAN_POINT ( 'NONE',  ( 66.18398860626901126, 28.73617430169833753, 5.000000000000000000 ) ) ;
#116868=ORIENTED_EDGE ( 'NONE', *, *, #120751, .F. ) ;
#116869=CARTESIAN_POINT ( 'NONE',  ( 1.499999999999987566, -4.216083040037250207, -7.486842126848659795 ) ) ;
#116872=FACE_BOUND ( 'NONE', #117547, .T. ) ;
#116873=LINE ( 'NONE', #69848, #98861 ) ;
#116874=DIRECTION ( 'NONE',  ( -0.000000000000000000, 0.000000000000000000, 1.000000000000000000 ) ) ;
#116875=DIRECTION ( 'NONE',  ( -1.000000000000000000, 0.000000000000000000, 0.000000000000000000 ) ) ;
#116876=VERTEX_POINT ( 'NONE', #125998 ) ;
#116877=DIRECTION ( 'NONE',  ( -0.000000000000000000, -0.3543493200069152693, 0.9351131265310292928 ) ) ;
#116878=ORIENTED_EDGE ( 'NONE', *, *, #7806, .F. ) ;
#116880=ORIENTED_EDGE ( 'NONE', *, *, #47196, .T. ) ;
#116881=CARTESIAN_POINT ( 'NONE',  ( -32.99999999999975842, 14.58746187583908771, 4.000000000000000000 ) ) ;
#116883=EDGE_CURVE ( 'NONE', #119248, #62339, #104195, .T. ) ;
#116884=VECTOR ( 'NONE', #138232, 999.9999999999998863 ) ;
#116886=ORIENTED_EDGE ( 'NONE', *, *, #50563, .F. ) ;
#116887=LINE ( 'NONE', #60400, #14036 ) ;
#116888=VECTOR ( 'NONE', #126965, 1000.000000000000000 ) ;
#116889=LINE ( 'NONE', #74848, #121314 ) ;
#116891=LINE ( 'NONE', #105986, #63049 ) ;
#116892=ADVANCED_FACE ( 'NONE', ( #25962 ), #83944, .F. ) ;
#116893=( BOUNDED_CURVE ( )  B_SPLINE_CURVE ( 3, ( #35847, #90174, #11151, #122082 ),
 .UNSPECIFIED., .F., .F. ) 
 B_SPLINE_CURVE_WITH_KNOTS ( ( 4, 4 ),
 ( 1.964434688349484537, 3.503810798801452187 ),
 .UNSPECIFIED. ) 
 CURVE ( )  GEOMETRIC_REPRESENTATION_ITEM ( )  RATIONAL_B_SPLINE_CURVE ( ( 1.000000000000000000, 0.8120851936182271746, 0.8120851936182271746, 1.000000000000000000 ) ) 
 REPRESENTATION_ITEM ( '' )  );
#116895=VECTOR ( 'NONE', #47988, 1000.000000000000000 ) ;
#116896=CARTESIAN_POINT ( 'NONE',  ( 14.99999999999989519, 7.559798855135672291, 4.979909187984731922 ) ) ;
#116898=DIRECTION ( 'NONE',  ( 0.7071067811865486830, -0.7071067811865464625, -0.000000000000000000 ) ) ;
#116899=DIRECTION ( 'NONE',  ( -0.000000000000000000, 0.3543493200069153248, 0.9351131265310292928 ) ) ;
#116900=VERTEX_POINT ( 'NONE', #128144 ) ;
#116901=ORIENTED_EDGE ( 'NONE', *, *, #25455, .F. ) ;
#116902=LINE ( 'NONE', #8114, #47404 ) ;
#116904=VERTEX_POINT ( 'NONE', #17220 ) ;
#116905=ORIENTED_EDGE ( 'NONE', *, *, #95340, .F. ) ;
#116906=ORIENTED_EDGE ( 'NONE', *, *, #98238, .F. ) ;
#116907=DIRECTION ( 'NONE',  ( 1.000000000000000000, 0.000000000000000000, 0.000000000000000000 ) ) ;
#116911=DIRECTION ( 'NONE',  ( -0.6830127018922181881, 0.6830127018922202975, -0.2588190451025214056 ) ) ;
#116914=VECTOR ( 'NONE', #8297, 1000.000000000000227 ) ;
#116916=VECTOR ( 'NONE', #39739, 1000.000000000000000 ) ;
#116919=CARTESIAN_POINT ( 'NONE',  ( 36.48921356237310221, -27.52281430457080802, 5.000000000000000000 ) ) ;
#116921=LINE ( 'NONE', #17589, #9545 ) ;
#116922=EDGE_CURVE ( 'NONE', #122443, #40992, #60030, .T. ) ;
#116923=CARTESIAN_POINT ( 'NONE',  ( -5.999999999999958256, 4.552185695429124657, 5.000000000000000000 ) ) ;
#116924=CARTESIAN_POINT ( 'NONE',  ( 54.18398860626899705, 28.73617430169825226, 5.000000000000000000 ) ) ;
#116925=EDGE_LOOP ( 'NONE', ( #62606, #139409, #90575, #113438 ) ) ;
#116926=CARTESIAN_POINT ( 'NONE',  ( 0.000000000000000000, 0.000000000000000000, 5.000000000000000000 ) ) ;
#116927=ORIENTED_EDGE ( 'NONE', *, *, #21501, .F. ) ;
#116928=FACE_OUTER_BOUND ( 'NONE', #18202, .T. ) ;
#116929=DIRECTION ( 'NONE',  ( 0.3543493200069162685, -0.000000000000000000, -0.9351131265310288487 ) ) ;
#116930=CARTESIAN_POINT ( 'NONE',  ( 38.53839644629405115, -9.740707523384177335, 17.74957260769619793 ) ) ;
#116931=VERTEX_POINT ( 'NONE', #71614 ) ;
#116932=CARTESIAN_POINT ( 'NONE',  ( 36.48921356237310221, -27.52281430457080802, 5.000000000000000000 ) ) ;
#116933=CARTESIAN_POINT ( 'NONE',  ( -11.51078643762690490, -27.52281430457047406, 5.000000000000000000 ) ) ;
#116934=CARTESIAN_POINT ( 'NONE',  ( -36.48921356237310221, -27.52281430457080802, 5.000000000000000000 ) ) ;
#116935=EDGE_LOOP ( 'NONE', ( #15619, #18403, #117413, #119680 ) ) ;
#116936=FACE_OUTER_BOUND ( 'NONE', #51493, .T. ) ;
#116938=DIRECTION ( 'NONE',  ( 0.7071067811865487940, -0.7071067811865463515, 0.000000000000000000 ) ) ;
#116940=CARTESIAN_POINT ( 'NONE',  ( -21.08491323193748812, -12.74070752338414891, 18.74364270924349185 ) ) ;
#116941=CARTESIAN_POINT ( 'NONE',  ( -22.49999999999984013, 5.696342897626483825, -7.587980461218449157 ) ) ;
#116942=EDGE_CURVE ( 'NONE', #79481, #90561, #125154, .T. ) ;
#116943=ORIENTED_EDGE ( 'NONE', *, *, #19785, .T. ) ;
#116944=ORIENTED_EDGE ( 'NONE', *, *, #90137, .T. ) ;
#116945=DIRECTION ( 'NONE',  ( 0.6830127018922180770, -0.6830127018922204085, -0.2588190451025213501 ) ) ;
#116946=CARTESIAN_POINT ( 'NONE',  ( -36.29974487139159578, -27.71228299555231445, 4.000000000000000000 ) ) ;
#116947=EDGE_CURVE ( 'NONE', #15939, #27059, #37564, .T. ) ;
#116948=ADVANCED_FACE ( 'NONE', ( #91919 ), #26670, .F. ) ;
#116950=PLANE ( 'NONE',  #120000 ) ;
#116951=CARTESIAN_POINT ( 'NONE',  ( -51.48921356237309510, -27.52281430457091460, 5.000000000000000000 ) ) ;
#116952=LINE ( 'NONE', #17618, #52926 ) ;
#116953=FACE_OUTER_BOUND ( 'NONE', #136536, .T. ) ;
#116954=ORIENTED_EDGE ( 'NONE', *, *, #18748, .F. ) ;
#116955=EDGE_CURVE ( 'NONE', #34380, #59881, #15059, .T. ) ;
#116956=DIRECTION ( 'NONE',  ( -0.000000000000000000, -0.3543493200069152693, 0.9351131265310292928 ) ) ;
#116957=CARTESIAN_POINT ( 'NONE',  ( 38.99451991528749062, 28.92564299267965211, 4.000000000000000000 ) ) ;
#116958=CARTESIAN_POINT ( 'NONE',  ( -13.49999999999990408, 7.466399257802187606, 5.000000000000000000 ) ) ;
#116959=FACE_OUTER_BOUND ( 'NONE', #59817, .T. ) ;
#116964=CARTESIAN_POINT ( 'NONE',  ( 29.99999999999979039, 12.25461709320623349, -10.07315571508690333 ) ) ;
#116965=ORIENTED_EDGE ( 'NONE', *, *, #102468, .F. ) ;
#116966=EDGE_LOOP ( 'NONE', ( #126211, #13176, #19877, #43457 ) ) ;
#116967=CARTESIAN_POINT ( 'NONE',  ( 36.29974487139159578, -27.71228299555231445, 4.000000000000000000 ) ) ;
#116968=EDGE_CURVE ( 'NONE', #117536, #112494, #117713, .T. ) ;
#116969=LINE ( 'NONE', #73486, #43885 ) ;
#116970=CARTESIAN_POINT ( 'NONE',  ( 3.299744871391591339, -27.71228299555208352, 4.000000000000000000 ) ) ;
#116971=LINE ( 'NONE', #19091, #136600 ) ;
#116972=DIRECTION ( 'NONE',  ( -0.000000000000000000, -0.3543493200069152693, 0.9351131265310292928 ) ) ;
#116973=PLANE ( 'NONE',  #66213 ) ;
#116974=ORIENTED_EDGE ( 'NONE', *, *, #94692, .T. ) ;
#116976=CARTESIAN_POINT ( 'NONE',  ( -12.18398860626900060, 28.73617430169795739, 5.000000000000000000 ) ) ;
#116977=EDGE_CURVE ( 'NONE', #75725, #56540, #81072, .T. ) ;
#116979=CARTESIAN_POINT ( 'NONE',  ( 21.48921356237309155, -27.52281430457070499, 5.000000000000000000 ) ) ;
#116980=CARTESIAN_POINT ( 'NONE',  ( 34.47516574401890921, 6.028067341115750821, 4.998110765256834398 ) ) ;
#116983=DIRECTION ( 'NONE',  ( -1.000000000000000000, 0.000000000000000000, -0.000000000000000000 ) ) ;
#116984=ORIENTED_EDGE ( 'NONE', *, *, #111138, .T. ) ;
#116985=VERTEX_POINT ( 'NONE', #49161 ) ;
#116987=CARTESIAN_POINT ( 'NONE',  ( -14.51078643762690490, -27.52281430457045275, 5.000000000000000000 ) ) ;
#116989=CARTESIAN_POINT ( 'NONE',  ( 32.29289321881323360, 2.259292476615696099, 5.000000000000000000 ) ) ;
#116990=ADVANCED_FACE ( 'NONE', ( #103490 ), #83198, .F. ) ;
#116992=ORIENTED_EDGE ( 'NONE', *, *, #108285, .F. ) ;
#116993=CARTESIAN_POINT ( 'NONE',  ( -33.48921356237309510, -27.52281430457078670, 5.000000000000000000 ) ) ;
#116994=EDGE_CURVE ( 'NONE', #12991, #12275, #28102, .T. ) ;
#116995=EDGE_CURVE ( 'NONE', #91273, #110128, #139013, .T. ) ;
#116996=VECTOR ( 'NONE', #102187, 1000.000000000000114 ) ;
#116997=CARTESIAN_POINT ( 'NONE',  ( -51.18398860626899705, 28.73617430169823095, 5.000000000000000000 ) ) ;
#116999=ORIENTED_EDGE ( 'NONE', *, *, #86418, .T. ) ;
#117000=DIRECTION ( 'NONE',  ( -0.7071067811865486830, -0.7071067811865464625, 0.000000000000000000 ) ) ;
#117001=EDGE_LOOP ( 'NONE', ( #106367, #132057, #47986, #94909 ) ) ;
#117004=EDGE_CURVE ( 'NONE', #65419, #125983, #29506, .T. ) ;
#117005=CARTESIAN_POINT ( 'NONE',  ( -33.79289321881321939, 18.75929247661552068, 5.000000000000000000 ) ) ;
#117006=LINE ( 'NONE', #37325, #118326 ) ;
#117007=CARTESIAN_POINT ( 'NONE',  ( 23.51078643762690490, -27.52281430457038880, 5.000000000000000000 ) ) ;
#117008=EDGE_CURVE ( 'NONE', #28348, #85531, #9904, .T. ) ;
#117009=CARTESIAN_POINT ( 'NONE',  ( -3.328169399223503078, -21.74070752338406010, 4.000000000000000000 ) ) ;
#117010=CARTESIAN_POINT ( 'NONE',  ( -23.99999999999982947, -15.41253812416059610, 4.000000000000000000 ) ) ;
#117011=ORIENTED_EDGE ( 'NONE', *, *, #86948, .F. ) ;
#117012=CARTESIAN_POINT ( 'NONE',  ( -21.70710678118640047, 20.25929247661551713, 5.000000000000000000 ) ) ;
#117013=CARTESIAN_POINT ( 'NONE',  ( -39.48921356237310221, -27.52281430457082934, 5.000000000000000000 ) ) ;
#117014=DIRECTION ( 'NONE',  ( 0.7071067811865486830, -0.7071067811865464625, -0.000000000000000000 ) ) ;
#117015=DIRECTION ( 'NONE',  ( -0.000000000000000000, 0.3543493200069153248, 0.9351131265310292928 ) ) ;
#117016=VECTOR ( 'NONE', #8717, 1000.000000000000000 ) ;
#117020=VECTOR ( 'NONE', #66267, 1000.000000000000000 ) ;
#117022=DIRECTION ( 'NONE',  ( 0.000000000000000000, 0.000000000000000000, 1.000000000000000000 ) ) ;
#117023=CARTESIAN_POINT ( 'NONE',  ( -28.49999999999978684, 4.087461875839202285, 4.000000000000000000 ) ) ;
#117024=DIRECTION ( 'NONE',  ( -2.781805975412905890E-17, 0.3543493200069152693, 0.9351131265310292928 ) ) ;
#117025=CARTESIAN_POINT ( 'NONE',  ( -26.56319896779154988, -12.74070752338415247, 9.898150129686436927 ) ) ;
#117026=CARTESIAN_POINT ( 'NONE',  ( -35.57672154193625147, 11.25929247661560240, 17.85071094206592690 ) ) ;
#117027=ORIENTED_EDGE ( 'NONE', *, *, #9579, .F. ) ;
#117028=ORIENTED_EDGE ( 'NONE', *, *, #19958, .F. ) ;
#117030=CARTESIAN_POINT ( 'NONE',  ( 33.18398860626899705, 28.73617430169810305, 5.000000000000000000 ) ) ;
#117032=ADVANCED_FACE ( 'NONE', ( #131704 ), #96879, .F. ) ;
#117033=VERTEX_POINT ( 'NONE', #64301 ) ;
#117034=VERTEX_POINT ( 'NONE', #75203 ) ;
#117035=CARTESIAN_POINT ( 'NONE',  ( 3.411614905948293419, 22.22500000000000142, 4.777194822843816802 ) ) ;
#117036=ORIENTED_EDGE ( 'NONE', *, *, #43394, .T. ) ;
#117037=DIRECTION ( 'NONE',  ( 0.7071067811865487940, 0.7071067811865463515, 0.000000000000000000 ) ) ;
#117038=CARTESIAN_POINT ( 'NONE',  ( 34.75611968250419181, 4.705650698524001641, 4.955485411084875835 ) ) ;
#117039=FACE_BOUND ( 'NONE', #95022, .T. ) ;
#117040=PLANE ( 'NONE',  #110335 ) ;
#117042=CARTESIAN_POINT ( 'NONE',  ( 28.49999999999980460, 1.087461875839230707, 4.000000000000000000 ) ) ;
#117043=DIRECTION ( 'NONE',  ( 0.7071067811865487940, 0.7071067811865463515, 0.000000000000000000 ) ) ;
#117045=SHAPE_DEFINITION_REPRESENTATION ( #6386, #103311 ) ;
#117046=ORIENTED_EDGE ( 'NONE', *, *, #9550, .T. ) ;
#117048=ORIENTED_EDGE ( 'NONE', *, *, #26619, .F. ) ;
#117050=ORIENTED_EDGE ( 'NONE', *, *, #28958, .F. ) ;
#117052=CARTESIAN_POINT ( 'NONE',  ( -34.92500000000001137, -22.22500000000000142, 4.500000000000000888 ) ) ;
#117053=DIRECTION ( 'NONE',  ( 0.7071067811865486830, -0.7071067811865464625, -0.000000000000000000 ) ) ;
#117054=ORIENTED_EDGE ( 'NONE', *, *, #142390, .F. ) ;
#117055=CARTESIAN_POINT ( 'NONE',  ( -17.51078643762690845, -27.52281430457043143, 5.000000000000000000 ) ) ;
#117057=LINE ( 'NONE', #51119, #82111 ) ;
#117058=CARTESIAN_POINT ( 'NONE',  ( 14.99999999999988809, -13.06887692260767331, 4.000000000000000000 ) ) ;
#117059=CARTESIAN_POINT ( 'NONE',  ( -34.49999999999976552, -8.945670655168967755, 4.994342998332164996 ) ) ;
#117062=CARTESIAN_POINT ( 'NONE',  ( -0.005480084712502889671, 28.92564299267938210, 4.000000000000000000 ) ) ;
#117063=ORIENTED_EDGE ( 'NONE', *, *, #75338, .F. ) ;
#117064=ORIENTED_EDGE ( 'NONE', *, *, #60359, .T. ) ;
#117068=( BOUNDED_CURVE ( )  B_SPLINE_CURVE ( 3, ( #48861, #78626, #113368, #58355 ),
 .UNSPECIFIED., .F., .T. ) 
 B_SPLINE_CURVE_WITH_KNOTS ( ( 4, 4 ),
 ( 2.779374508378134934, 4.199602562396838934 ),
 .UNSPECIFIED. ) 
 CURVE ( )  GEOMETRIC_REPRESENTATION_ITEM ( )  RATIONAL_B_SPLINE_CURVE ( ( 1.000000000000000000, 0.8388583629366627159, 0.8388583629366627159, 1.000000000000000000 ) ) 
 REPRESENTATION_ITEM ( '' )  );
#117069=AXIS2_PLACEMENT_3D ( 'NONE', #19493, #41978, #7150 ) ;
#117072=ORIENTED_EDGE ( 'NONE', *, *, #68491, .F. ) ;
#117074=DIRECTION ( 'NONE',  ( 1.000000000000000000, 0.000000000000000000, 0.000000000000000000 ) ) ;
#117075=ORIENTED_EDGE ( 'NONE', *, *, #103513, .T. ) ;
#117076=FACE_OUTER_BOUND ( 'NONE', #89140, .T. ) ;
#117077=DIRECTION ( 'NONE',  ( -0.6830127018922180770, -0.6830127018922204085, -0.2588190451025213501 ) ) ;
#117078=LINE ( 'NONE', #7600, #49480 ) ;
#117079=ORIENTED_EDGE ( 'NONE', *, *, #107012, .T. ) ;
#117080=ORIENTED_EDGE ( 'NONE', *, *, #67751, .F. ) ;
#117081=LINE ( 'NONE', #102676, #102423 ) ;
#117083=ORIENTED_EDGE ( 'NONE', *, *, #40526, .F. ) ;
#117084=FACE_OUTER_BOUND ( 'NONE', #109362, .T. ) ;
#117085=EDGE_LOOP ( 'NONE', ( #91519, #136688, #108089, #11654 ) ) ;
#117086=EDGE_LOOP ( 'NONE', ( #67108, #25864, #52296, #129897, #97052, #85015 ) ) ;
#117088=ORIENTED_EDGE ( 'NONE', *, *, #17658, .T. ) ;
#117089=EDGE_CURVE ( 'NONE', #41151, #45672, #54179, .T. ) ;
#117090=DIRECTION ( 'NONE',  ( -0.7071067811865486830, -0.7071067811865464625, 0.000000000000000000 ) ) ;
#117091=DIRECTION ( 'NONE',  ( 0.3543493200069162685, -0.000000000000000000, -0.9351131265310288487 ) ) ;
#117093=LINE ( 'NONE', #6167, #84455 ) ;
#117094=CARTESIAN_POINT ( 'NONE',  ( 68.99451991528748351, 28.92564299267986172, 4.000000000000000000 ) ) ;
#117095=EDGE_CURVE ( 'NONE', #33358, #13774, #20055, .T. ) ;
#117096=ADVANCED_FACE ( 'NONE', ( #97626 ), #17894, .F. ) ;
#117097=VERTEX_POINT ( 'NONE', #141886 ) ;
#117099=ORIENTED_EDGE ( 'NONE', *, *, #17332, .F. ) ;
#117100=LINE ( 'NONE', #114934, #30854 ) ;
#117103=EDGE_CURVE ( 'NONE', #142129, #64647, #120062, .T. ) ;
#117105=CARTESIAN_POINT ( 'NONE',  ( 33.48921356237309510, -27.52281430457078670, 5.000000000000000000 ) ) ;
#117106=VECTOR ( 'NONE', #38576, 1000.000000000000227 ) ;
#117107=ORIENTED_EDGE ( 'NONE', *, *, #123364, .T. ) ;
#117108=CARTESIAN_POINT ( 'NONE',  ( -45.48921356237309510, -27.52281430457087197, 5.000000000000000000 ) ) ;
#117110=EDGE_LOOP ( 'NONE', ( #74530, #46834, #46215 ) ) ;
#117111=VECTOR ( 'NONE', #65333, 1000.000000000000000 ) ;
#117112=ORIENTED_EDGE ( 'NONE', *, *, #1464, .F. ) ;
#117114=VERTEX_POINT ( 'NONE', #117921 ) ;
#117115=DIRECTION ( 'NONE',  ( -0.3543493200069162685, -0.000000000000000000, -0.9351131265310288487 ) ) ;
#117116=DIRECTION ( 'NONE',  ( 1.000000000000000000, 0.000000000000000000, 0.000000000000000000 ) ) ;
#117117=FACE_OUTER_BOUND ( 'NONE', #125968, .T. ) ;
#117119=DIRECTION ( 'NONE',  ( 0.6830127018922180770, -0.6830127018922204085, -0.2588190451025213501 ) ) ;
#117122=CARTESIAN_POINT ( 'NONE',  ( -29.99999999999978328, 4.552185695429124657, 5.000000000000000000 ) ) ;
#117123=ADVANCED_FACE ( 'NONE', ( #62898 ), #107078, .F. ) ;
#117124=PLANE ( 'NONE',  #122506 ) ;
#117125=CARTESIAN_POINT ( 'NONE',  ( -29.57659687702524920, -22.22500000000000142, 2.973290122897137344 ) ) ;
#117127=CARTESIAN_POINT ( 'NONE',  ( 48.29974487139158867, -27.71228299555239971, 4.000000000000000000 ) ) ;
#117128=VERTEX_POINT ( 'NONE', #44741 ) ;
#117129=DIRECTION ( 'NONE',  ( -0.7071067811865486830, -0.7071067811865464625, -0.000000000000000000 ) ) ;
#117130=VERTEX_POINT ( 'NONE', #135295 ) ;
#117131=CARTESIAN_POINT ( 'NONE',  ( -36.18398860626899705, 28.73617430169812437, 5.000000000000000000 ) ) ;
#117132=DIRECTION ( 'NONE',  ( 0.7071067811865487940, 0.7071067811865463515, 0.000000000000000000 ) ) ;
#117133=ORIENTED_EDGE ( 'NONE', *, *, #116508, .F. ) ;
#117134=CARTESIAN_POINT ( 'NONE',  ( 26.20666063542134339, 21.75929247661549581, 4.998822639870700968 ) ) ;
#117135=LINE ( 'NONE', #17814, #51862 ) ;
#117136=VERTEX_POINT ( 'NONE', #46895 ) ;
#117137=ORIENTED_EDGE ( 'NONE', *, *, #98549, .F. ) ;
#117138=LINE ( 'NONE', #6206, #97564 ) ;
#117139=LINE ( 'NONE', #119284, #120803 ) ;
#117140=EDGE_CURVE ( 'NONE', #57564, #130156, #120808, .T. ) ;
#117141=DIRECTION ( 'NONE',  ( -0.7071067811865486830, -0.7071067811865464625, 0.000000000000000000 ) ) ;
#117143=CARTESIAN_POINT ( 'NONE',  ( 20.99999999999986144, -10.06887692260770173, 4.000000000000000000 ) ) ;
#117144=ORIENTED_EDGE ( 'NONE', *, *, #75121, .T. ) ;
#117146=DIRECTION ( 'NONE',  ( 0.7071067811865486830, -0.7071067811865464625, -0.000000000000000000 ) ) ;
#117149=ADVANCED_FACE ( 'NONE', ( #21515 ), #67917, .F. ) ;
#117150=VECTOR ( 'NONE', #63552, 1000.000000000000227 ) ;
#117151=CARTESIAN_POINT ( 'NONE',  ( 8.915086768062332467, -12.74070752338415602, 18.74364270924356290 ) ) ;
#117154=EDGE_CURVE ( 'NONE', #12722, #21741, #1837, .T. ) ;
#117157=EDGE_CURVE ( 'NONE', #114197, #40900, #76632, .T. ) ;
#117158=LINE ( 'NONE', #74410, #45486 ) ;
#117159=DIRECTION ( 'NONE',  ( 0.6830127018922180770, -0.6830127018922204085, -0.2588190451025213501 ) ) ;
#117160=DIRECTION ( 'NONE',  ( -0.7071067811865486830, -0.7071067811865464625, 0.000000000000000000 ) ) ;
#117161=ORIENTED_EDGE ( 'NONE', *, *, #66926, .T. ) ;
#117162=LINE ( 'NONE', #95425, #90567 ) ;
#117163=EDGE_CURVE ( 'NONE', #40291, #117136, #67161, .T. ) ;
#117164=CARTESIAN_POINT ( 'NONE',  ( 59.99451991528749772, 28.92564299267980132, 4.000000000000000000 ) ) ;
#117166=DIRECTION ( 'NONE',  ( 0.6830127018922181881, 0.6830127018922202975, -0.2588190451025214056 ) ) ;
#117167=ORIENTED_EDGE ( 'NONE', *, *, #92334, .T. ) ;
#117168=LINE ( 'NONE', #132390, #32181 ) ;
#117170=ORIENTED_EDGE ( 'NONE', *, *, #51628, .F. ) ;
#117172=VERTEX_POINT ( 'NONE', #46146 ) ;
#117174=ORIENTED_EDGE ( 'NONE', *, *, #31460, .T. ) ;
#117177=DIRECTION ( 'NONE',  ( -0.6830127018922180770, -0.6830127018922204085, -0.2588190451025213501 ) ) ;
#117178=CARTESIAN_POINT ( 'NONE',  ( 3.328169399223503966, 14.25929247661557397, 4.000000000000000000 ) ) ;
#117179=LINE ( 'NONE', #62126, #17640 ) ;
#117180=VERTEX_POINT ( 'NONE', #68605 ) ;
#117181=DIRECTION ( 'NONE',  ( 1.000000000000000000, 0.000000000000000000, 0.000000000000000000 ) ) ;
#117182=CARTESIAN_POINT ( 'NONE',  ( -12.48921356237309155, -27.52281430457064104, 5.000000000000000000 ) ) ;
#117183=ORIENTED_EDGE ( 'NONE', *, *, #73037, .T. ) ;
#117185=DIRECTION ( 'NONE',  ( 1.000000000000000000, 0.000000000000000000, 0.000000000000000000 ) ) ;
#117186=CARTESIAN_POINT ( 'NONE',  ( 51.18398860626899705, 28.73617430169823095, 5.000000000000000000 ) ) ;
#117187=LINE ( 'NONE', #6974, #67845 ) ;
#117188=ORIENTED_EDGE ( 'NONE', *, *, #74596, .T. ) ;
#117189=ORIENTED_EDGE ( 'NONE', *, *, #119693, .F. ) ;
#117190=ADVANCED_FACE ( 'NONE', ( #99773 ), #79513, .T. ) ;
#117191=VECTOR ( 'NONE', #115911, 1000.000000000000000 ) ;
#117194=LINE ( 'NONE', #107054, #78929 ) ;
#117195=CARTESIAN_POINT ( 'NONE',  ( -23.99999999999982947, -21.84840872380826937, 2.849755605029552274 ) ) ;
#117197=VECTOR ( 'NONE', #18385, 999.9999999999998863 ) ;
#117198=VECTOR ( 'NONE', #90855, 1000.000000000000000 ) ;
#117199=DIRECTION ( 'NONE',  ( 0.7071067811865487940, 0.7071067811865463515, 0.000000000000000000 ) ) ;
#117200=ORIENTED_EDGE ( 'NONE', *, *, #136123, .F. ) ;
#117201=VECTOR ( 'NONE', #31280, 1000.000000000000000 ) ;
#117202=ORIENTED_EDGE ( 'NONE', *, *, #72116, .T. ) ;
#117203=ORIENTED_EDGE ( 'NONE', *, *, #82428, .T. ) ;
#117204=ORIENTED_EDGE ( 'NONE', *, *, #47966, .T. ) ;
#117205=VECTOR ( 'NONE', #45526, 1000.000000000000227 ) ;
#117206=ADVANCED_FACE ( 'NONE', ( #110625 ), #13453, .F. ) ;
#117208=ADVANCED_FACE ( 'NONE', ( #88935 ), #133152, .F. ) ;
#117209=ORIENTED_EDGE ( 'NONE', *, *, #106150, .F. ) ;
#117210=PLANE ( 'NONE',  #62165 ) ;
#117211=LINE ( 'NONE', #139006, #72741 ) ;
#117212=CARTESIAN_POINT ( 'NONE',  ( -34.92500000000001137, -15.89852273831279028, -9.446427897663618012 ) ) ;
#117213=DIRECTION ( 'NONE',  ( -4.681814790819591790E-17, -0.3543493200069152693, 0.9351131265310292928 ) ) ;
#117214=CARTESIAN_POINT ( 'NONE',  ( -39.48921356237310221, -27.52281430457082934, 5.000000000000000000 ) ) ;
#117215=ORIENTED_EDGE ( 'NONE', *, *, #36606, .F. ) ;
#117216=PLANE ( 'NONE',  #3146 ) ;
#117217=DIRECTION ( 'NONE',  ( 0.3543493200069162685, -0.000000000000000000, -0.9351131265310288487 ) ) ;
#117218=ORIENTED_EDGE ( 'NONE', *, *, #24136, .F. ) ;
#117219=CARTESIAN_POINT ( 'NONE',  ( 14.29289321881336150, -18.74070752338409562, 5.000000000000000000 ) ) ;
#117220=ORIENTED_EDGE ( 'NONE', *, *, #33529, .F. ) ;
#117221=EDGE_CURVE ( 'NONE', #22222, #112964, #123704, .T. ) ;
#117223=ORIENTED_EDGE ( 'NONE', *, *, #2884, .F. ) ;
#117224=VERTEX_POINT ( 'NONE', #134576 ) ;
#117226=ORIENTED_EDGE ( 'NONE', *, *, #86740, .F. ) ;
#117229=CARTESIAN_POINT ( 'NONE',  ( -32.01088028653925477, -22.02621442084248216, 4.990779571109222879 ) ) ;
#117232=DIRECTION ( 'NONE',  ( 0.7071067811865487940, 0.7071067811865463515, -0.000000000000000000 ) ) ;
#117233=CARTESIAN_POINT ( 'NONE',  ( -30.48921356237309510, -27.52281430457076894, 5.000000000000000000 ) ) ;
#117234=PLANE ( 'NONE',  #74164 ) ;
#117235=AXIS2_PLACEMENT_3D ( 'NONE', #23197, #2147, #67482 ) ;
#117236=PLANE ( 'NONE',  #114113 ) ;
#117240=DIRECTION ( 'NONE',  ( 0.7071067811865487940, 0.7071067811865463515, 0.000000000000000000 ) ) ;
#117242=ORIENTED_EDGE ( 'NONE', *, *, #106212, .F. ) ;
#117243=ORIENTED_EDGE ( 'NONE', *, *, #2410, .T. ) ;
#117247=DIRECTION ( 'NONE',  ( 0.3543493200069162685, -0.000000000000000000, -0.9351131265310288487 ) ) ;
#117249=LINE ( 'NONE', #62933, #57936 ) ;
#117251=EDGE_CURVE ( 'NONE', #88267, #53631, #24358, .T. ) ;
#117252=ORIENTED_EDGE ( 'NONE', *, *, #99314, .F. ) ;
#117254=VERTEX_POINT ( 'NONE', #78049 ) ;
#117255=VECTOR ( 'NONE', #18260, 1000.000000000000000 ) ;
#117256=ADVANCED_FACE ( 'NONE', ( #99042 ), #143280, .T. ) ;
#117259=LINE ( 'NONE', #16529, #16919 ) ;
#117260=ADVANCED_FACE ( 'NONE', ( #89611 ), #101199, .F. ) ;
#117261=DIRECTION ( 'NONE',  ( -0.7071067811865486830, -0.7071067811865464625, 0.000000000000000000 ) ) ;
#117265=ORIENTED_EDGE ( 'NONE', *, *, #10564, .T. ) ;
#117266=EDGE_CURVE ( 'NONE', #81792, #72669, #3300, .T. ) ;
#117267=AXIS2_PLACEMENT_3D ( 'NONE', #62624, #16966, #61239 ) ;
#117268=EDGE_LOOP ( 'NONE', ( #114740, #109448, #101533, #40679 ) ) ;
#117269=DIRECTION ( 'NONE',  ( -0.7071067811865487940, 0.7071067811865463515, -0.000000000000000000 ) ) ;
#117270=DIRECTION ( 'NONE',  ( 0.7071067811865487940, 0.7071067811865463515, 0.000000000000000000 ) ) ;
#117271=DIRECTION ( 'NONE',  ( -0.000000000000000000, 0.000000000000000000, 1.000000000000000000 ) ) ;
#117272=EDGE_CURVE ( 'NONE', #22612, #52625, #138125, .T. ) ;
#117273=DIRECTION ( 'NONE',  ( -0.6830127018922181881, 0.6830127018922202975, -0.2588190451025214056 ) ) ;
#117274=CARTESIAN_POINT ( 'NONE',  ( 0.000000000000000000, 0.000000000000000000, 5.000000000000000000 ) ) ;
#117275=DIRECTION ( 'NONE',  ( 0.6830127018922180770, -0.6830127018922204085, -0.2588190451025213501 ) ) ;
#117276=DIRECTION ( 'NONE',  ( -0.000000000000000000, -0.3543493200069152693, 0.9351131265310292928 ) ) ;
#117277=EDGE_CURVE ( 'NONE', #13287, #44234, #15576, .T. ) ;
#117278=LINE ( 'NONE', #62231, #97227 ) ;
#117279=VECTOR ( 'NONE', #6827, 999.9999999999998863 ) ;
#117280=CARTESIAN_POINT ( 'NONE',  ( -12.70701326429296252, -21.74070752338406010, 4.999753212805220670 ) ) ;
#117281=CARTESIAN_POINT ( 'NONE',  ( 18.32816939922340893, 20.25929247661551358, 4.000000000000000000 ) ) ;
#117282=ORIENTED_EDGE ( 'NONE', *, *, #135644, .F. ) ;
#117283=DIRECTION ( 'NONE',  ( 0.7071067811865487940, 0.7071067811865463515, -0.000000000000000000 ) ) ;
#117284=DIRECTION ( 'NONE',  ( -0.7071067811865486830, -0.7071067811865464625, 0.000000000000000000 ) ) ;
#117285=ORIENTED_EDGE ( 'NONE', *, *, #14780, .F. ) ;
#117286=ADVANCED_FACE ( 'NONE', ( #71446 ), #61327, .F. ) ;
#117288=DIRECTION ( 'NONE',  ( -0.000000000000000000, 0.3543493200069153248, 0.9351131265310292928 ) ) ;
#117289=ORIENTED_EDGE ( 'NONE', *, *, #128662, .F. ) ;
#117291=ADVANCED_FACE ( 'NONE', ( #125833 ), #59857, .F. ) ;
#117292=DIRECTION ( 'NONE',  ( -0.000000000000000000, 0.3543493200069153248, 0.9351131265310292928 ) ) ;
#117293=DIRECTION ( 'NONE',  ( 0.3543493200069162685, -0.000000000000000000, -0.9351131265310288487 ) ) ;
#117294=VERTEX_POINT ( 'NONE', #6131 ) ;
#117295=DIRECTION ( 'NONE',  ( 0.6830127018922180770, -0.6830127018922204085, -0.2588190451025213501 ) ) ;
#117297=ORIENTED_EDGE ( 'NONE', *, *, #75041, .T. ) ;
#117298=EDGE_CURVE ( 'NONE', #106679, #115779, #114898, .T. ) ;
#117299=VECTOR ( 'NONE', #15707, 999.9999999999998863 ) ;
#117301=DIRECTION ( 'NONE',  ( 0.7071067811865487940, 0.7071067811865463515, 0.000000000000000000 ) ) ;
#117304=PLANE ( 'NONE',  #25401 ) ;
#117305=DIRECTION ( 'NONE',  ( -0.000000000000000000, -0.3543493200069152693, 0.9351131265310292928 ) ) ;
#117306=LINE ( 'NONE', #94837, #60794 ) ;
#117307=DIRECTION ( 'NONE',  ( 0.7071067811865486830, -0.7071067811865464625, -0.000000000000000000 ) ) ;
#117308=CARTESIAN_POINT ( 'NONE',  ( 5.913098576467837653, -22.22500000000000142, 20.47508215891419781 ) ) ;
#117311=CARTESIAN_POINT ( 'NONE',  ( -23.20666063542136470, 21.75929247661548516, 4.998822639870711626 ) ) ;
#117312=VECTOR ( 'NONE', #36432, 1000.000000000000227 ) ;
#117313=PLANE ( 'NONE',  #81355 ) ;
#117314=LINE ( 'NONE', #118756, #50199 ) ;
#117315=EDGE_LOOP ( 'NONE', ( #113557, #535, #41098, #74459 ) ) ;
#117316=ORIENTED_EDGE ( 'NONE', *, *, #63006, .T. ) ;
#117319=ORIENTED_EDGE ( 'NONE', *, *, #68903, .T. ) ;
#117322=CARTESIAN_POINT ( 'NONE',  ( -8.999999999999932498, -0.4125381241607516403, 4.000000000000000000 ) ) ;
#117323=DIRECTION ( 'NONE',  ( 0.7071067811865486830, -0.7071067811865464625, -0.000000000000000000 ) ) ;
#117324=VERTEX_POINT ( 'NONE', #27202 ) ;
#117325=DIRECTION ( 'NONE',  ( -0.7071067811865486830, -0.7071067811865464625, 0.000000000000000000 ) ) ;
#117326=DIRECTION ( 'NONE',  ( 0.7071067811865487940, 0.7071067811865463515, 0.000000000000000000 ) ) ;
#117327=LINE ( 'NONE', #49281, #9332 ) ;
#117328=DIRECTION ( 'NONE',  ( -0.000000000000000000, -0.3543493200069152693, 0.9351131265310292928 ) ) ;
#117329=CARTESIAN_POINT ( 'NONE',  ( 0.000000000000000000, 0.000000000000000000, 5.000000000000000000 ) ) ;
#117330=FACE_OUTER_BOUND ( 'NONE', #50632, .T. ) ;
#117331=VECTOR ( 'NONE', #100710, 1000.000000000000000 ) ;
#117332=PLANE ( 'NONE',  #3575 ) ;
#117333=LINE ( 'NONE', #105055, #49318 ) ;
#117334=DIRECTION ( 'NONE',  ( -0.000000000000000000, 0.3543493200069153248, 0.9351131265310292928 ) ) ;
#117335=LINE ( 'NONE', #107191, #47626 ) ;
#117336=EDGE_CURVE ( 'NONE', #45356, #80320, #127226, .T. ) ;
#117337=CARTESIAN_POINT ( 'NONE',  ( -34.92500000000001137, 1.701930566820992308, 4.500000000000000888 ) ) ;
#117338=EDGE_LOOP ( 'NONE', ( #15397, #22516, #25129, #22760 ) ) ;
#117341=VERTEX_POINT ( 'NONE', #37387 ) ;
#117342=ADVANCED_FACE ( 'NONE', ( #104028 ), #70060, .F. ) ;
#117344=VECTOR ( 'NONE', #56197, 1000.000000000000000 ) ;
#117345=DIRECTION ( 'NONE',  ( -0.6830127018922181881, 0.6830127018922202975, -0.2588190451025214056 ) ) ;
#117346=VERTEX_POINT ( 'NONE', #115602 ) ;
#117347=DIRECTION ( 'NONE',  ( 0.7071067811865487940, -0.7071067811865463515, 0.000000000000000000 ) ) ;
#117348=FACE_OUTER_BOUND ( 'NONE', #28714, .T. ) ;
#117350=EDGE_LOOP ( 'NONE', ( #114380, #69190, #94619, #40305 ) ) ;
#117351=EDGE_CURVE ( 'NONE', #73090, #73943, #93187, .T. ) ;
#117352=PLANE ( 'NONE',  #99833 ) ;
#117353=ORIENTED_EDGE ( 'NONE', *, *, #88314, .F. ) ;
#117354=DIRECTION ( 'NONE',  ( -0.000000000000000000, 0.3543493200069153248, 0.9351131265310292928 ) ) ;
#117355=AXIS2_PLACEMENT_3D ( 'NONE', #10336, #140844, #53891 ) ;
#117356=LINE ( 'NONE', #63742, #97799 ) ;
#117357=FACE_OUTER_BOUND ( 'NONE', #16486, .T. ) ;
#117358=ORIENTED_EDGE ( 'NONE', *, *, #122105, .T. ) ;
#117359=ORIENTED_EDGE ( 'NONE', *, *, #2258, .T. ) ;
#117361=EDGE_CURVE ( 'NONE', #138157, #98423, #83033, .T. ) ;
#117362=ORIENTED_EDGE ( 'NONE', *, *, #136662, .T. ) ;
#117363=LINE ( 'NONE', #106473, #72327 ) ;
#117367=ORIENTED_EDGE ( 'NONE', *, *, #11952, .F. ) ;
#117368=VECTOR ( 'NONE', #101534, 1000.000000000000227 ) ;
#117369=ORIENTED_EDGE ( 'NONE', *, *, #65507, .T. ) ;
#117370=DIRECTION ( 'NONE',  ( -0.6830127018922181881, 0.6830127018922202975, -0.2588190451025214056 ) ) ;
#117371=VERTEX_POINT ( 'NONE', #116371 ) ;
#117372=ORIENTED_EDGE ( 'NONE', *, *, #59584, .F. ) ;
#117373=CARTESIAN_POINT ( 'NONE',  ( 25.82816939922335209, 18.75929247661552068, 4.000000000000000000 ) ) ;
#117375=EDGE_CURVE ( 'NONE', #76282, #45436, #36654, .T. ) ;
#117376=VERTEX_POINT ( 'NONE', #16306 ) ;
#117377=LINE ( 'NONE', #84105, #52912 ) ;
#117378=VECTOR ( 'NONE', #94581, 1000.000000000000000 ) ;
#117379=DIRECTION ( 'NONE',  ( -0.7071067811865486830, -0.7071067811865464625, -0.000000000000000000 ) ) ;
#117380=DIRECTION ( 'NONE',  ( 0.000000000000000000, 1.000000000000000000, 0.000000000000000000 ) ) ;
#117381=CARTESIAN_POINT ( 'NONE',  ( 33.79333936457825160, 21.75929247661550647, 4.998822639870711626 ) ) ;
#117382=ORIENTED_EDGE ( 'NONE', *, *, #16461, .F. ) ;
#117383=CARTESIAN_POINT ( 'NONE',  ( 11.29298673570687050, -21.74070752338406365, 4.999753212805220670 ) ) ;
#117385=PLANE ( 'NONE',  #38450 ) ;
#117386=ORIENTED_EDGE ( 'NONE', *, *, #32275, .F. ) ;
#117388=CARTESIAN_POINT ( 'NONE',  ( -24.59263130292903554, 0.9595543924999635488, 5.000000000000000000 ) ) ;
#117389=DIRECTION ( 'NONE',  ( 0.7071067811865487940, 0.7071067811865463515, 0.000000000000000000 ) ) ;
#117390=EDGE_CURVE ( 'NONE', #3647, #58008, #14188, .T. ) ;
#117391=ORIENTED_EDGE ( 'NONE', *, *, #32502, .F. ) ;
#117392=LINE ( 'NONE', #95660, #50486 ) ;
#117393=ORIENTED_EDGE ( 'NONE', *, *, #1300, .F. ) ;
#117394=VERTEX_POINT ( 'NONE', #17059 ) ;
#117395=VECTOR ( 'NONE', #3943, 1000.000000000000000 ) ;
#117398=VECTOR ( 'NONE', #58636, 1000.000000000000000 ) ;
#117400=CARTESIAN_POINT ( 'NONE',  ( 41.99451991528749062, 28.92564299267967343, 4.000000000000000000 ) ) ;
#117401=DIRECTION ( 'NONE',  ( 0.7071067811865487940, 0.7071067811865463515, 0.000000000000000000 ) ) ;
#117402=CARTESIAN_POINT ( 'NONE',  ( 8.999999999999937828, 7.007997736742456851, -8.085015511992091675 ) ) ;
#117404=DIRECTION ( 'NONE',  ( -0.000000000000000000, 0.000000000000000000, 1.000000000000000000 ) ) ;
#117405=CARTESIAN_POINT ( 'NONE',  ( 0.000000000000000000, 0.000000000000000000, 5.000000000000000000 ) ) ;
#117406=PLANE ( 'NONE',  #129153 ) ;
#117407=AXIS2_PLACEMENT_3D ( 'NONE', #55708, #1965, #57156 ) ;
#117408=LINE ( 'NONE', #52175, #60871 ) ;
#117409=CARTESIAN_POINT ( 'NONE',  ( -27.29974487139158512, -27.71228299555225405, 4.000000000000000000 ) ) ;
#117412=ORIENTED_EDGE ( 'NONE', *, *, #13366, .T. ) ;
#117413=ORIENTED_EDGE ( 'NONE', *, *, #61525, .F. ) ;
#117414=ORIENTED_EDGE ( 'NONE', *, *, #55796, .T. ) ;
#117415=ORIENTED_EDGE ( 'NONE', *, *, #24159, .T. ) ;
#117418=ORIENTED_EDGE ( 'NONE', *, *, #18560, .F. ) ;
#117419=FACE_OUTER_BOUND ( 'NONE', #140482, .T. ) ;
#117420=CARTESIAN_POINT ( 'NONE',  ( -14.24715658456393541, 6.719242673238161601, 5.000000000000000000 ) ) ;
#117421=LINE ( 'NONE', #103689, #80344 ) ;
#117422=CARTESIAN_POINT ( 'NONE',  ( -24.18398860626899705, 28.73617430169804265, 5.000000000000000000 ) ) ;
#117424=AXIS2_PLACEMENT_3D ( 'NONE', #53246, #64872, #111190 ) ;
#117426=ORIENTED_EDGE ( 'NONE', *, *, #67938, .T. ) ;
#117427=CARTESIAN_POINT ( 'NONE',  ( -21.79289321881330110, 12.75929247661558996, 5.000000000000000000 ) ) ;
#117428=DIRECTION ( 'NONE',  ( 0.6830127018922180770, -0.6830127018922204085, -0.2588190451025213501 ) ) ;
#117429=EDGE_CURVE ( 'NONE', #74780, #9436, #60603, .T. ) ;
#117430=VECTOR ( 'NONE', #38327, 1000.000000000000000 ) ;
#117432=ORIENTED_EDGE ( 'NONE', *, *, #101240, .T. ) ;
#117434=( BOUNDED_CURVE ( )  B_SPLINE_CURVE ( 3, ( #106859, #71404, #137377, #6800 ),
 .UNSPECIFIED., .F., .T. ) 
 B_SPLINE_CURVE_WITH_KNOTS ( ( 4, 4 ),
 ( 1.901594255663606736, 1.933014472006571838 ),
 .UNSPECIFIED. ) 
 CURVE ( )  GEOMETRIC_REPRESENTATION_ITEM ( )  RATIONAL_B_SPLINE_CURVE ( ( 1.000000000000000000, 0.9999177325257867510, 0.9999177325257867510, 1.000000000000000000 ) ) 
 REPRESENTATION_ITEM ( '' )  );
#117435=CARTESIAN_POINT ( 'NONE',  ( 23.99999999999983302, -0.2811185226894059586, -5.995736974527568819 ) ) ;
#117436=EDGE_CURVE ( 'NONE', #53397, #117371, #103323, .T. ) ;
#117438=CARTESIAN_POINT ( 'NONE',  ( -2.510786437626908008, -27.52281430457053446, 5.000000000000000000 ) ) ;
#117439=VERTEX_POINT ( 'NONE', #6843 ) ;
#117440=EDGE_LOOP ( 'NONE', ( #15088, #96779, #111858, #94573 ) ) ;
#117443=ORIENTED_EDGE ( 'NONE', *, *, #140298, .T. ) ;
#117445=DIRECTION ( 'NONE',  ( -0.7071067811865486830, 0.7071067811865464625, 0.000000000000000000 ) ) ;
#117446=LINE ( 'NONE', #18117, #71987 ) ;
#117447=DIRECTION ( 'NONE',  ( -0.7071067811865487940, 0.7071067811865463515, 0.000000000000000000 ) ) ;
#117448=DIRECTION ( 'NONE',  ( 0.6830127018922181881, 0.6830127018922202975, -0.2588190451025214056 ) ) ;
#117449=ADVANCED_FACE ( 'NONE', ( #53234 ), #18439, .F. ) ;
#117450=DIRECTION ( 'NONE',  ( 1.000000000000000000, 0.000000000000000000, 0.000000000000000000 ) ) ;
#117452=LINE ( 'NONE', #127654, #115393 ) ;
#117453=CARTESIAN_POINT ( 'NONE',  ( 0.4892135623730947680, -27.52281430457055578, 5.000000000000000000 ) ) ;
#117455=VECTOR ( 'NONE', #74759, 999.9999999999998863 ) ;
#117456=ORIENTED_EDGE ( 'NONE', *, *, #88891, .F. ) ;
#117457=CARTESIAN_POINT ( 'NONE',  ( -12.18398860626900060, 28.73617430169795739, 5.000000000000000000 ) ) ;
#117458=CARTESIAN_POINT ( 'NONE',  ( 7.171830600776422315, 18.75929247661553489, 4.000000000000000000 ) ) ;
#117459=VERTEX_POINT ( 'NONE', #138850 ) ;
#117460=EDGE_CURVE ( 'NONE', #65131, #65842, #51126, .T. ) ;
#117462=EDGE_LOOP ( 'NONE', ( #22492, #17919, #80468, #128512, #60462 ) ) ;
#117463=EDGE_CURVE ( 'NONE', #57964, #51885, #40267, .T. ) ;
#117464=LINE ( 'NONE', #52230, #58631 ) ;
#117465=CARTESIAN_POINT ( 'NONE',  ( 34.92499999999998295, -5.405284025385218349, -5.470147491473914769 ) ) ;
#117467=CARTESIAN_POINT ( 'NONE',  ( 30.24169458425169310, 0.7592924766157138627, 14.37146558664976048 ) ) ;
#117468=ADVANCED_FACE ( 'NONE', ( #83773 ), #140957, .F. ) ;
#117469=LINE ( 'NONE', #138547, #105400 ) ;
#117470=CARTESIAN_POINT ( 'NONE',  ( -34.49999999999976552, 18.05432934483075513, 4.994342998332167660 ) ) ;
#117472=FACE_OUTER_BOUND ( 'NONE', #62262, .T. ) ;
#117473=FACE_OUTER_BOUND ( 'NONE', #12476, .T. ) ;
#117474=LINE ( 'NONE', #97134, #127729 ) ;
#117476=DIRECTION ( 'NONE',  ( -0.000000000000000000, -0.3543493200069152693, 0.9351131265310292928 ) ) ;
#117479=CARTESIAN_POINT ( 'NONE',  ( 54.48921356237310221, -27.52281430457093236, 5.000000000000000000 ) ) ;
#117480=LINE ( 'NONE', #18154, #102140 ) ;
#117482=ORIENTED_EDGE ( 'NONE', *, *, #71108, .T. ) ;
#117483=ORIENTED_EDGE ( 'NONE', *, *, #22690, .F. ) ;
#117484=ORIENTED_EDGE ( 'NONE', *, *, #118336, .T. ) ;
#117487=ORIENTED_EDGE ( 'NONE', *, *, #65353, .T. ) ;
#117488=ORIENTED_EDGE ( 'NONE', *, *, #61599, .T. ) ;
#117489=EDGE_CURVE ( 'NONE', #75592, #51436, #7584, .T. ) ;
#117490=CARTESIAN_POINT ( 'NONE',  ( 18.18398860626898994, 28.73617430169800002, 5.000000000000000000 ) ) ;
#117491=CARTESIAN_POINT ( 'NONE',  ( 18.29974487139159223, -27.71228299555219010, 4.000000000000000000 ) ) ;
#117492=ORIENTED_EDGE ( 'NONE', *, *, #56820, .T. ) ;
#117494=CARTESIAN_POINT ( 'NONE',  ( 32.99999999999976552, -19.22509904557633575, 1.855685503482255250 ) ) ;
#117495=LINE ( 'NONE', #62450, #141254 ) ;
#117497=CARTESIAN_POINT ( 'NONE',  ( 21.48921356237309155, -27.52281430457070499, 5.000000000000000000 ) ) ;
#117498=CARTESIAN_POINT ( 'NONE',  ( 18.93838080770422039, 22.22500000000000142, -15.41084850694827324 ) ) ;
#117500=ORIENTED_EDGE ( 'NONE', *, *, #110234, .F. ) ;
#117501=LINE ( 'NONE', #40696, #23238 ) ;
#117502=DIRECTION ( 'NONE',  ( 0.6830127018922180770, -0.6830127018922204085, -0.2588190451025213501 ) ) ;
#117503=EDGE_CURVE ( 'NONE', #64975, #59481, #72915, .T. ) ;
#117505=CARTESIAN_POINT ( 'NONE',  ( 0.005480084712502889671, 28.92564299267938210, 4.000000000000000000 ) ) ;
#117510=EDGE_CURVE ( 'NONE', #55935, #8580, #95321, .T. ) ;
#117512=LINE ( 'NONE', #18186, #39329 ) ;
#117513=ORIENTED_EDGE ( 'NONE', *, *, #73489, .F. ) ;
#117514=EDGE_LOOP ( 'NONE', ( #23822, #24223, #31423, #22106, #117063 ) ) ;
#117516=VERTEX_POINT ( 'NONE', #42406 ) ;
#117517=CARTESIAN_POINT ( 'NONE',  ( 0.4892135623730947680, -27.52281430457055578, 5.000000000000000000 ) ) ;
#117518=CARTESIAN_POINT ( 'NONE',  ( -36.88837638105219696, 9.759292476615614831, 17.35367589129221244 ) ) ;
#117519=VECTOR ( 'NONE', #58975, 999.9999999999998863 ) ;
#117520=CARTESIAN_POINT ( 'NONE',  ( 0.000000000000000000, 0.000000000000000000, 5.000000000000000000 ) ) ;
#117521=CARTESIAN_POINT ( 'NONE',  ( -5.510786437626906675, -27.52281430457051314, 5.000000000000000000 ) ) ;
#117525=ORIENTED_EDGE ( 'NONE', *, *, #21743, .F. ) ;
#117526=EDGE_CURVE ( 'NONE', #44496, #128691, #139586, .T. ) ;
#117527=DIRECTION ( 'NONE',  ( 0.7071067811865486830, -0.7071067811865464625, -0.000000000000000000 ) ) ;
#117528=VERTEX_POINT ( 'NONE', #96028 ) ;
#117529=DIRECTION ( 'NONE',  ( -0.7071067811865486830, -0.7071067811865464625, -0.000000000000000000 ) ) ;
#117530=CARTESIAN_POINT ( 'NONE',  ( 27.75860074219777118, 21.72500000000000142, 5.000000000000000000 ) ) ;
#117531=CARTESIAN_POINT ( 'NONE',  ( 30.18398860626900060, 28.73617430169808173, 5.000000000000000000 ) ) ;
#117532=DIRECTION ( 'NONE',  ( -0.6830127018922180770, -0.6830127018922204085, -0.2588190451025214056 ) ) ;
#117533=ORIENTED_EDGE ( 'NONE', *, *, #16872, .T. ) ;
#117535=ADVANCED_FACE ( 'NONE', ( #19197 ), #97448, .F. ) ;
#117536=VERTEX_POINT ( 'NONE', #8972 ) ;
#117537=LINE ( 'NONE', #87083, #63316 ) ;
#117538=DIRECTION ( 'NONE',  ( 0.7071067811865487940, 0.7071067811865463515, 0.000000000000000000 ) ) ;
#117539=DIRECTION ( 'NONE',  ( -0.7071067811865487940, 0.7071067811865463515, 0.000000000000000000 ) ) ;
#117541=LINE ( 'NONE', #129154, #78818 ) ;
#117543=ORIENTED_EDGE ( 'NONE', *, *, #54600, .F. ) ;
#117544=FACE_OUTER_BOUND ( 'NONE', #31361, .T. ) ;
#117545=FACE_OUTER_BOUND ( 'NONE', #34137, .T. ) ;
#117546=ORIENTED_EDGE ( 'NONE', *, *, #20239, .F. ) ;
#117547=EDGE_LOOP ( 'NONE', ( #104165, #46719, #5116, #32735 ) ) ;
#117548=ORIENTED_EDGE ( 'NONE', *, *, #7092, .T. ) ;
#117549=DIRECTION ( 'NONE',  ( 0.7071067811865487940, 0.7071067811865463515, -0.000000000000000000 ) ) ;
#117550=EDGE_CURVE ( 'NONE', #81264, #60957, #64857, .T. ) ;
#117552=LINE ( 'NONE', #126320, #15845 ) ;
#117553=CARTESIAN_POINT ( 'NONE',  ( -9.299744871391588674, -27.71228299555212971, 4.000000000000000000 ) ) ;
#117554=CARTESIAN_POINT ( 'NONE',  ( -9.345819385248065103, 22.22500000000000142, 14.69290773491317026 ) ) ;
#117556=FACE_BOUND ( 'NONE', #30725, .T. ) ;
#117559=ADVANCED_FACE ( 'NONE', ( #31505 ), #140267, .F. ) ;
#117560=ORIENTED_EDGE ( 'NONE', *, *, #136347, .F. ) ;
#117561=CARTESIAN_POINT ( 'NONE',  ( 78.18398860626899705, 28.73617430169841924, 5.000000000000000000 ) ) ;
#117562=ORIENTED_EDGE ( 'NONE', *, *, #68444, .F. ) ;
#117563=VERTEX_POINT ( 'NONE', #30056 ) ;
#117565=ORIENTED_EDGE ( 'NONE', *, *, #120562, .F. ) ;
#117567=ORIENTED_EDGE ( 'NONE', *, *, #77483, .T. ) ;
#117568=VECTOR ( 'NONE', #88928, 1000.000000000000000 ) ;
#117569=DIRECTION ( 'NONE',  ( 0.6830127018922180770, -0.6830127018922204085, -0.2588190451025213501 ) ) ;
#117570=DIRECTION ( 'NONE',  ( 0.6830127018922180770, -0.6830127018922204085, -0.2588190451025213501 ) ) ;
#117571=ORIENTED_EDGE ( 'NONE', *, *, #105988, .F. ) ;
#117572=DIRECTION ( 'NONE',  ( 0.6830127018922180770, -0.6830127018922204085, -0.2588190451025213501 ) ) ;
#117573=EDGE_CURVE ( 'NONE', #68343, #82336, #106169, .T. ) ;
#117574=VECTOR ( 'NONE', #77088, 1000.000000000000000 ) ;
#117575=CARTESIAN_POINT ( 'NONE',  ( -63.18398860626900415, 28.73617430169831621, 5.000000000000000000 ) ) ;
#117577=LINE ( 'NONE', #137239, #114078 ) ;
#117578=DIRECTION ( 'NONE',  ( -0.7071067811865486830, -0.7071067811865464625, 0.000000000000000000 ) ) ;
#117579=VERTEX_POINT ( 'NONE', #63452 ) ;
#117580=ORIENTED_EDGE ( 'NONE', *, *, #114378, .F. ) ;
#117583=CARTESIAN_POINT ( 'NONE',  ( 36.18398860626899705, 28.73617430169812437, 5.000000000000000000 ) ) ;
#117584=ORIENTED_EDGE ( 'NONE', *, *, #47220, .T. ) ;
#117585=VERTEX_POINT ( 'NONE', #107620 ) ;
#117586=VECTOR ( 'NONE', #28638, 1000.000000000000000 ) ;
#117587=ORIENTED_EDGE ( 'NONE', *, *, #118722, .T. ) ;
#117588=FACE_OUTER_BOUND ( 'NONE', #48255, .T. ) ;
#117590=ORIENTED_EDGE ( 'NONE', *, *, #137147, .F. ) ;
#117591=DIRECTION ( 'NONE',  ( -0.000000000000000000, 0.3543493200069153248, 0.9351131265310292928 ) ) ;
#117593=VECTOR ( 'NONE', #6465, 1000.000000000000227 ) ;
#117594=FACE_OUTER_BOUND ( 'NONE', #79092, .T. ) ;
#117600=ADVANCED_FACE ( 'NONE', ( #24201 ), #43808, .F. ) ;
#117601=CARTESIAN_POINT ( 'NONE',  ( 28.17183060077628198, 12.75929247661558286, 4.000000000000000000 ) ) ;
#117602=CARTESIAN_POINT ( 'NONE',  ( 6.299744871391586898, -27.71228299555210484, 4.000000000000000000 ) ) ;
#117603=DIRECTION ( 'NONE',  ( -0.3543493200069162685, -0.000000000000000000, -0.9351131265310288487 ) ) ;
#117604=EDGE_LOOP ( 'NONE', ( #19856, #23827, #75780, #67676, #63393 ) ) ;
#117605=DIRECTION ( 'NONE',  ( 1.000000000000000000, 0.000000000000000000, 0.000000000000000000 ) ) ;
#117606=ORIENTED_EDGE ( 'NONE', *, *, #64001, .F. ) ;
#117607=LINE ( 'NONE', #87160, #63572 ) ;
#117608=DIRECTION ( 'NONE',  ( -0.000000000000000000, 0.000000000000000000, 1.000000000000000000 ) ) ;
#117609=EDGE_CURVE ( 'NONE', #66395, #129172, #133676, .T. ) ;
#117610=EDGE_CURVE ( 'NONE', #95492, #99130, #43108, .T. ) ;
#117611=CARTESIAN_POINT ( 'NONE',  ( 0.000000000000000000, 0.000000000000000000, 5.000000000000000000 ) ) ;
#117612=ORIENTED_EDGE ( 'NONE', *, *, #128465, .T. ) ;
#117613=PLANE ( 'NONE',  #49617 ) ;
#117614=LINE ( 'NONE', #40814, #102095 ) ;
#117616=ORIENTED_EDGE ( 'NONE', *, *, #19483, .T. ) ;
#117618=FACE_OUTER_BOUND ( 'NONE', #21632, .T. ) ;
#117619=CARTESIAN_POINT ( 'NONE',  ( 11.20710678118647330, 12.75929247661558996, 5.000000000000000000 ) ) ;
#117620=AXIS2_PLACEMENT_3D ( 'NONE', #75605, #30681, #20472 ) ;
#117621=LINE ( 'NONE', #40141, #105001 ) ;
#117622=EDGE_CURVE ( 'NONE', #133767, #87458, #33530, .T. ) ;
#117624=ORIENTED_EDGE ( 'NONE', *, *, #62882, .F. ) ;
#117625=EDGE_CURVE ( 'NONE', #103619, #100067, #76453, .T. ) ;
#117626=ORIENTED_EDGE ( 'NONE', *, *, #86751, .F. ) ;
#117628=DIRECTION ( 'NONE',  ( -0.7071067811865486830, -0.7071067811865464625, 0.000000000000000000 ) ) ;
#117631=FACE_OUTER_BOUND ( 'NONE', #52919, .T. ) ;
#117632=DIRECTION ( 'NONE',  ( 1.000000000000000000, 0.000000000000000000, 0.000000000000000000 ) ) ;
#117633=ADVANCED_FACE ( 'NONE', ( #45971 ), #98877, .F. ) ;
#117634=DIRECTION ( 'NONE',  ( -0.6830127018922181881, 0.6830127018922202975, -0.2588190451025214056 ) ) ;
#117635=VERTEX_POINT ( 'NONE', #77868 ) ;
#117636=LINE ( 'NONE', #60475, #46511 ) ;
#117638=CARTESIAN_POINT ( 'NONE',  ( 34.49999999999976552, -17.56887692260763245, 4.000000000000000000 ) ) ;
#117640=VECTOR ( 'NONE', #37580, 1000.000000000000227 ) ;
#117641=FACE_OUTER_BOUND ( 'NONE', #36718, .T. ) ;
#117643=LINE ( 'NONE', #96597, #48750 ) ;
#117644=VECTOR ( 'NONE', #102544, 1000.000000000000000 ) ;
#117646=FACE_OUTER_BOUND ( 'NONE', #111981, .T. ) ;
#117647=ORIENTED_EDGE ( 'NONE', *, *, #27169, .T. ) ;
#117650=DIRECTION ( 'NONE',  ( 0.7071067811865487940, 0.7071067811865463515, 0.000000000000000000 ) ) ;
#117651=CARTESIAN_POINT ( 'NONE',  ( 22.82816939922338051, -11.24070752338416668, 4.000000000000000000 ) ) ;
#117652=DIRECTION ( 'NONE',  ( 0.3543493200069164351, 2.781805975412904658E-17, -0.9351131265310288487 ) ) ;
#117653=LINE ( 'NONE', #127883, #27847 ) ;
#117657=EDGE_CURVE ( 'NONE', #109897, #64492, #22722, .T. ) ;
#117658=CARTESIAN_POINT ( 'NONE',  ( 60.48921356237309510, -27.52281430457097500, 5.000000000000000000 ) ) ;
#117659=CARTESIAN_POINT ( 'NONE',  ( 1.499999999999987566, -1.533600742197726463, 5.000000000000000000 ) ) ;
#117660=EDGE_CURVE ( 'NONE', #16867, #31094, #111176, .T. ) ;
#117661=PLANE ( 'NONE',  #31016 ) ;
#117662=FACE_OUTER_BOUND ( 'NONE', #97789, .T. ) ;
#117663=FACE_OUTER_BOUND ( 'NONE', #49, .T. ) ;
#117664=CARTESIAN_POINT ( 'NONE',  ( 14.51078643762690490, -27.52281430457045275, 5.000000000000000000 ) ) ;
#117666=EDGE_CURVE ( 'NONE', #45590, #84277, #111931, .T. ) ;
#117667=FACE_OUTER_BOUND ( 'NONE', #47538, .T. ) ;
#117668=VERTEX_POINT ( 'NONE', #1676 ) ;
#117670=VECTOR ( 'NONE', #51658, 1000.000000000000227 ) ;
#117672=LINE ( 'NONE', #138043, #86429 ) ;
#117673=CARTESIAN_POINT ( 'NONE',  ( 0.000000000000000000, -21.72500000000000142, 4.500000000000000888 ) ) ;
#117674=DIRECTION ( 'NONE',  ( 0.7071067811865487940, 0.7071067811865463515, 0.000000000000000000 ) ) ;
#117675=EDGE_LOOP ( 'NONE', ( #69727, #134291, #47533, #71449 ) ) ;
#117676=PLANE ( 'NONE',  #60742 ) ;
#117678=ORIENTED_EDGE ( 'NONE', *, *, #124622, .T. ) ;
#117679=CARTESIAN_POINT ( 'NONE',  ( 8.816011393731004731, 28.73617430169781173, 5.000000000000000000 ) ) ;
#117680=ORIENTED_EDGE ( 'NONE', *, *, #115619, .F. ) ;
#117681=ORIENTED_EDGE ( 'NONE', *, *, #129563, .F. ) ;
#117682=FACE_OUTER_BOUND ( 'NONE', #127722, .T. ) ;
#117683=VECTOR ( 'NONE', #80360, 1000.000000000000000 ) ;
#117684=VECTOR ( 'NONE', #109441, 1000.000000000000000 ) ;
#117686=CARTESIAN_POINT ( 'NONE',  ( -6.489213562373093325, -27.52281430457059841, 5.000000000000000000 ) ) ;
#117687=VECTOR ( 'NONE', #102629, 1000.000000000000000 ) ;
#117688=CARTESIAN_POINT ( 'NONE',  ( 16.49999999999988987, -7.533600742197658739, 5.000000000000000000 ) ) ;
#117689=CARTESIAN_POINT ( 'NONE',  ( -23.29298673570678702, -21.74070752338405299, 4.999753212805217117 ) ) ;
#117690=DIRECTION ( 'NONE',  ( 0.7071067811865487940, 0.7071067811865463515, 0.000000000000000000 ) ) ;
#117694=CARTESIAN_POINT ( 'NONE',  ( 15.70710678118643955, 8.259292476615634371, 5.000000000000000000 ) ) ;
#117696=CARTESIAN_POINT ( 'NONE',  ( -45.48921356237309510, -27.52281430457087197, 5.000000000000000000 ) ) ;
#117697=VECTOR ( 'NONE', #11493, 1000.000000000000000 ) ;
#117698=CARTESIAN_POINT ( 'NONE',  ( -29.34505516254599655, 5.259292476615672562, 12.77922209995886682 ) ) ;
#117699=VECTOR ( 'NONE', #80779, 999.9999999999998863 ) ;
#117700=ORIENTED_EDGE ( 'NONE', *, *, #101062, .T. ) ;
#117701=ORIENTED_EDGE ( 'NONE', *, *, #15473, .F. ) ;
#117702=PLANE ( 'NONE',  #31519 ) ;
#117705=CARTESIAN_POINT ( 'NONE',  ( -32.99451991528749062, 28.92564299267960948, 4.000000000000000000 ) ) ;
#117706=CARTESIAN_POINT ( 'NONE',  ( -34.49999999999976552, 1.464255608400471642, 4.994342998332163219 ) ) ;
#117707=VERTEX_POINT ( 'NONE', #35097 ) ;
#117708=VERTEX_POINT ( 'NONE', #79339 ) ;
#117709=VECTOR ( 'NONE', #85031, 1000.000000000000000 ) ;
#117711=DIRECTION ( 'NONE',  ( 0.7071067811865487940, -0.7071067811865463515, 0.000000000000000000 ) ) ;
#117713=( BOUNDED_CURVE ( )  B_SPLINE_CURVE ( 3, ( #93356, #104937, #3461, #49872 ),
 .UNSPECIFIED., .F., .F. ) 
 B_SPLINE_CURVE_WITH_KNOTS ( ( 4, 4 ),
 ( 5.390251506879594423, 5.422326034329064903 ),
 .UNSPECIFIED. ) 
 CURVE ( )  GEOMETRIC_REPRESENTATION_ITEM ( )  RATIONAL_B_SPLINE_CURVE ( ( 1.000000000000000000, 0.9999142705615216009, 0.9999142705615216009, 1.000000000000000000 ) ) 
 REPRESENTATION_ITEM ( '' )  );
#117714=EDGE_LOOP ( 'NONE', ( #59273, #98021, #17678, #18585 ) ) ;
#117715=AXIS2_PLACEMENT_3D ( 'NONE', #111264, #99680, #58390 ) ;
#117717=EDGE_LOOP ( 'NONE', ( #66523, #104920, #7108, #37215 ) ) ;
#117718=CARTESIAN_POINT ( 'NONE',  ( 18.32816939922338761, -18.74070752338410273, 4.000000000000000000 ) ) ;
#117719=VECTOR ( 'NONE', #97140, 1000.000000000000000 ) ;
#117720=VECTOR ( 'NONE', #12109, 999.9999999999998863 ) ;
#117721=VECTOR ( 'NONE', #107952, 1000.000000000000000 ) ;
#117722=CARTESIAN_POINT ( 'NONE',  ( 50.99451991528749062, 28.92564299267973738, 4.000000000000000000 ) ) ;
#117723=EDGE_CURVE ( 'NONE', #91253, #38197, #127060, .T. ) ;
#117724=FACE_BOUND ( 'NONE', #82962, .T. ) ;
#117726=CARTESIAN_POINT ( 'NONE',  ( 2.999999999999981792, -9.033600742197648970, 5.000000000000000000 ) ) ;
#117727=EDGE_CURVE ( 'NONE', #82657, #67930, #125662, .T. ) ;
#117728=DIRECTION ( 'NONE',  ( -0.6830127018922180770, 0.6830127018922202975, -0.2588190451025213501 ) ) ;
#117729=CARTESIAN_POINT ( 'NONE',  ( 54.18398860626899705, 28.73617430169825226, 5.000000000000000000 ) ) ;
#117730=EDGE_LOOP ( 'NONE', ( #48124, #42260, #142979, #116074 ) ) ;
#117731=VECTOR ( 'NONE', #77598, 1000.000000000000227 ) ;
#117732=VECTOR ( 'NONE', #76816, 1000.000000000000000 ) ;
#117734=ORIENTED_EDGE ( 'NONE', *, *, #4938, .F. ) ;
#117737=EDGE_LOOP ( 'NONE', ( #119328, #27228, #52810, #82831 ) ) ;
#117738=DIRECTION ( 'NONE',  ( 0.6830127018922180770, 0.6830127018922202975, -0.2588190451025213501 ) ) ;
#117739=EDGE_CURVE ( 'NONE', #103883, #86102, #49547, .T. ) ;
#117740=LINE ( 'NONE', #40940, #90648 ) ;
#117741=LINE ( 'NONE', #18425, #37476 ) ;
#117743=ADVANCED_FACE ( 'NONE', ( #27751 ), #101749, .F. ) ;
#117744=DIRECTION ( 'NONE',  ( -0.3543493200069162685, -0.000000000000000000, -0.9351131265310288487 ) ) ;
#117745=DIRECTION ( 'NONE',  ( 0.6830127018922180770, -0.6830127018922204085, -0.2588190451025213501 ) ) ;
#117746=CARTESIAN_POINT ( 'NONE',  ( 26.67183060077628909, 14.25929247661557220, 4.000000000000000000 ) ) ;
#117747=DIRECTION ( 'NONE',  ( 0.7071067811865487940, -0.7071067811865463515, 0.000000000000000000 ) ) ;
#117748=DIRECTION ( 'NONE',  ( -0.7071067811865486830, 0.7071067811865464625, 0.000000000000000000 ) ) ;
#117749=LINE ( 'NONE', #39538, #118721 ) ;
#117750=CARTESIAN_POINT ( 'NONE',  ( 54.48921356237310221, -27.52281430457093236, 5.000000000000000000 ) ) ;
#117751=EDGE_CURVE ( 'NONE', #36106, #51825, #21147, .T. ) ;
#117752=CARTESIAN_POINT ( 'NONE',  ( -2.999999999999981792, -16.02097659208072145, -11.96015758381207839 ) ) ;
#117753=ORIENTED_EDGE ( 'NONE', *, *, #39946, .T. ) ;
#117754=LINE ( 'NONE', #64856, #24070 ) ;
#117755=CARTESIAN_POINT ( 'NONE',  ( -33.18398860626899705, 28.73617430169810305, 5.000000000000000000 ) ) ;
#117756=EDGE_LOOP ( 'NONE', ( #22917, #18659, #14128 ) ) ;
#117758=ORIENTED_EDGE ( 'NONE', *, *, #113178, .F. ) ;
#117760=EDGE_CURVE ( 'NONE', #125114, #100892, #122381, .T. ) ;
#117761=ORIENTED_EDGE ( 'NONE', *, *, #35765, .T. ) ;
#117764=VERTEX_POINT ( 'NONE', #104602 ) ;
#117765=CARTESIAN_POINT ( 'NONE',  ( 18.51789069628991768, -2.771357050275779610, 4.325358181756080000 ) ) ;
#117766=ADVANCED_FACE ( 'NONE', ( #14005 ), #82872, .T. ) ;
#117768=DIRECTION ( 'NONE',  ( 0.6830127018922181881, 0.6830127018922202975, -0.2588190451025214056 ) ) ;
#117769=FACE_OUTER_BOUND ( 'NONE', #3759, .T. ) ;
#117770=DIRECTION ( 'NONE',  ( 0.7071067811865486830, -0.7071067811865464625, -0.000000000000000000 ) ) ;
#117771=ORIENTED_EDGE ( 'NONE', *, *, #73425, .F. ) ;
#117772=ORIENTED_EDGE ( 'NONE', *, *, #133253, .F. ) ;
#117773=DIRECTION ( 'NONE',  ( 0.7071067811865487940, 0.7071067811865463515, -0.000000000000000000 ) ) ;
#117774=EDGE_CURVE ( 'NONE', #92653, #53159, #58308, .T. ) ;
#117776=ORIENTED_EDGE ( 'NONE', *, *, #51807, .F. ) ;
#117777=PLANE ( 'NONE',  #112954 ) ;
#117778=ORIENTED_EDGE ( 'NONE', *, *, #53495, .F. ) ;
#117779=AXIS2_PLACEMENT_3D ( 'NONE', #110150, #129777, #76123 ) ;
#117780=ORIENTED_EDGE ( 'NONE', *, *, #127406, .F. ) ;
#117781=EDGE_LOOP ( 'NONE', ( #29647, #35695, #75922, #42053 ) ) ;
#117782=ORIENTED_EDGE ( 'NONE', *, *, #138310, .F. ) ;
#117783=CARTESIAN_POINT ( 'NONE',  ( 20.70025512860841133, -27.71228299555191654, 4.000000000000000000 ) ) ;
#117785=VECTOR ( 'NONE', #42188, 1000.000000000000000 ) ;
#117786=EDGE_CURVE ( 'NONE', #118176, #104855, #102490, .T. ) ;
#117787=CARTESIAN_POINT ( 'NONE',  ( -22.80981832425537448, -18.74070752338408852, 7.910009926591561324 ) ) ;
#117788=AXIS2_PLACEMENT_3D ( 'NONE', #56663, #89935, #34880 ) ;
#117789=CARTESIAN_POINT ( 'NONE',  ( -8.999999999999934275, -12.03360074219761522, 5.000000000000000000 ) ) ;
#117790=EDGE_CURVE ( 'NONE', #109084, #71690, #4506, .T. ) ;
#117791=CARTESIAN_POINT ( 'NONE',  ( -15.83829387547370438, -6.740707523384212863, 16.75550250614863756 ) ) ;
#117792=EDGE_LOOP ( 'NONE', ( #16676, #90882, #84248, #65595 ) ) ;
#117794=CARTESIAN_POINT ( 'NONE',  ( 28.49999999999981171, -20.94781430457062044, 5.000000000000000000 ) ) ;
#117795=EDGE_LOOP ( 'NONE', ( #17096, #112361, #118600, #66000 ) ) ;
#117797=LINE ( 'NONE', #6173, #132800 ) ;
#117798=PLANE ( 'NONE',  #46191 ) ;
#117799=CARTESIAN_POINT ( 'NONE',  ( 13.43359823057990354, 1.153863645259229909, 4.000000000000000000 ) ) ;
#117800=ORIENTED_EDGE ( 'NONE', *, *, #40694, .T. ) ;
#117801=CARTESIAN_POINT ( 'NONE',  ( 34.92499999999998295, -17.99387692260784988, 4.000000000000000000 ) ) ;
#117802=ADVANCED_FACE ( 'NONE', ( #135813 ), #3138, .F. ) ;
#117804=EDGE_LOOP ( 'NONE', ( #116071, #42726, #7393, #3955 ) ) ;
#117806=VERTEX_POINT ( 'NONE', #48099 ) ;
#117808=CARTESIAN_POINT ( 'NONE',  ( -45.48921356237309510, -27.52281430457087197, 5.000000000000000000 ) ) ;
#117809=DIRECTION ( 'NONE',  ( 0.7071067811865487940, 0.7071067811865463515, 0.000000000000000000 ) ) ;
#117810=AXIS2_PLACEMENT_3D ( 'NONE', #108723, #141385, #140658 ) ;
#117812=PLANE ( 'NONE',  #140008 ) ;
#117813=EDGE_CURVE ( 'NONE', #97758, #83926, #5265, .T. ) ;
#117816=CARTESIAN_POINT ( 'NONE',  ( -11.29387692260796072, 22.22500000000000142, 4.000000000000000000 ) ) ;
#117817=VECTOR ( 'NONE', #23377, 1000.000000000000227 ) ;
#117818=DIRECTION ( 'NONE',  ( -0.000000000000000000, 0.000000000000000000, 1.000000000000000000 ) ) ;
#117820=DIRECTION ( 'NONE',  ( -0.000000000000000000, -0.3543493200069152693, 0.9351131265310292928 ) ) ;
#117822=ORIENTED_EDGE ( 'NONE', *, *, #14051, .T. ) ;
#117823=CARTESIAN_POINT ( 'NONE',  ( -0.7928932188134485415, -17.24070752338410628, 5.000000000000000000 ) ) ;
#117824=PLANE ( 'NONE',  #107796 ) ;
#117825=ORIENTED_EDGE ( 'NONE', *, *, #34084, .T. ) ;
#117827=VECTOR ( 'NONE', #141780, 1000.000000000000000 ) ;
#117828=VECTOR ( 'NONE', #93244, 999.9999999999998863 ) ;
#117829=CARTESIAN_POINT ( 'NONE',  ( -51.18398860626899705, 28.73617430169823095, 5.000000000000000000 ) ) ;
#117830=CARTESIAN_POINT ( 'NONE',  ( -21.48921356237309155, -27.52281430457070499, 5.000000000000000000 ) ) ;
#117831=ORIENTED_EDGE ( 'NONE', *, *, #74482, .T. ) ;
#117832=DIRECTION ( 'NONE',  ( -0.7071067811865487940, 0.7071067811865463515, 0.000000000000000000 ) ) ;
#117833=CARTESIAN_POINT ( 'NONE',  ( -15.48921356237309510, -27.52281430457066236, 5.000000000000000000 ) ) ;
#117834=ORIENTED_EDGE ( 'NONE', *, *, #92811, .T. ) ;
#117835=ORIENTED_EDGE ( 'NONE', *, *, #140127, .T. ) ;
#117837=CARTESIAN_POINT ( 'NONE',  ( -6.516654386410399624, 22.22500000000000142, 4.500000000000000888 ) ) ;
#117838=VECTOR ( 'NONE', #52770, 1000.000000000000227 ) ;
#117839=CARTESIAN_POINT ( 'NONE',  ( -33.77004279457769798, 21.73644205237998506, 5.000000000000000888 ) ) ;
#117840=EDGE_CURVE ( 'NONE', #60276, #15282, #14741, .T. ) ;
#117842=DIRECTION ( 'NONE',  ( 0.6830127018922181881, 0.6830127018922202975, -0.2588190451025214056 ) ) ;
#117843=ADVANCED_FACE ( 'NONE', ( #27037 ), #71284, .T. ) ;
#117844=DIRECTION ( 'NONE',  ( -0.7071067811865486830, -0.7071067811865464625, 0.000000000000000000 ) ) ;
#117845=EDGE_LOOP ( 'NONE', ( #138292, #91411, #112010, #115554 ) ) ;
#117847=LINE ( 'NONE', #16394, #113298 ) ;
#117849=VECTOR ( 'NONE', #124089, 1000.000000000000227 ) ;
#117850=ORIENTED_EDGE ( 'NONE', *, *, #98660, .T. ) ;
#117851=PLANE ( 'NONE',  #113875 ) ;
#117852=VERTEX_POINT ( 'NONE', #37210 ) ;
#117854=CARTESIAN_POINT ( 'NONE',  ( -11.99999999999991296, 16.55218569542899587, 5.000000000000000000 ) ) ;
#117855=DIRECTION ( 'NONE',  ( 0.7071067811865486830, -0.7071067811865464625, -0.000000000000000000 ) ) ;
#117856=ORIENTED_EDGE ( 'NONE', *, *, #102626, .T. ) ;
#117857=FACE_OUTER_BOUND ( 'NONE', #57431, .T. ) ;
#117859=FACE_OUTER_BOUND ( 'NONE', #55064, .T. ) ;
#117860=ORIENTED_EDGE ( 'NONE', *, *, #99012, .F. ) ;
#117861=DIRECTION ( 'NONE',  ( 0.7071067811865486830, -0.7071067811865464625, -0.000000000000000000 ) ) ;
#117862=PLANE ( 'NONE',  #142593 ) ;
#117864=CARTESIAN_POINT ( 'NONE',  ( 0.1839886062690032631, 28.73617430169787568, 5.000000000000000000 ) ) ;
#117865=ORIENTED_EDGE ( 'NONE', *, *, #119877, .F. ) ;
#117866=ORIENTED_EDGE ( 'NONE', *, *, #20684, .T. ) ;
#117868=EDGE_LOOP ( 'NONE', ( #136717, #62702, #138974, #2085 ) ) ;
#117869=CARTESIAN_POINT ( 'NONE',  ( -16.49999999999988987, 1.030536316426491128, -5.498701923753763765 ) ) ;
#117870=DIRECTION ( 'NONE',  ( -0.7071067811865486830, -0.7071067811865464625, 0.000000000000000000 ) ) ;
#117871=DIRECTION ( 'NONE',  ( -0.7071067811865487940, 0.7071067811865463515, 0.000000000000000000 ) ) ;
#117872=ORIENTED_EDGE ( 'NONE', *, *, #19829, .T. ) ;
#117873=DIRECTION ( 'NONE',  ( -0.6830127018922181881, 0.6830127018922202975, -0.2588190451025214056 ) ) ;
#117874=DIRECTION ( 'NONE',  ( -0.7071067811865487940, 0.7071067811865463515, 0.000000000000000000 ) ) ;
#117875=ORIENTED_EDGE ( 'NONE', *, *, #131562, .F. ) ;
#117876=CARTESIAN_POINT ( 'NONE',  ( -24.91272823266826109, 2.053671025133813277, 5.000000000000000000 ) ) ;
#117877=VECTOR ( 'NONE', #94377, 1000.000000000000000 ) ;
#117878=CARTESIAN_POINT ( 'NONE',  ( 5.999999999999960032, -12.41253812416063340, 4.000000000000000000 ) ) ;
#117879=DIRECTION ( 'NONE',  ( -0.7071067811865486830, 0.7071067811865464625, 0.000000000000000000 ) ) ;
#117880=VECTOR ( 'NONE', #50052, 1000.000000000000000 ) ;
#117882=AXIS2_PLACEMENT_3D ( 'NONE', #96655, #64077, #86556 ) ;
#117883=ORIENTED_EDGE ( 'NONE', *, *, #124988, .T. ) ;
#117884=ORIENTED_EDGE ( 'NONE', *, *, #4928, .T. ) ;
#117885=AXIS2_PLACEMENT_3D ( 'NONE', #123699, #23642, #67913 ) ;
#117886=EDGE_CURVE ( 'NONE', #115165, #132568, #81460, .T. ) ;
#117888=EDGE_CURVE ( 'NONE', #132587, #55809, #75556, .T. ) ;
#117889=CARTESIAN_POINT ( 'NONE',  ( 27.70710678118635428, -6.740707523384216415, 5.000000000000000000 ) ) ;
#117890=DIRECTION ( 'NONE',  ( -0.000000000000000000, 0.3543493200069153248, 0.9351131265310292928 ) ) ;
#117891=LINE ( 'NONE', #73042, #27992 ) ;
#117893=VECTOR ( 'NONE', #111627, 1000.000000000000000 ) ;
#117895=( BOUNDED_CURVE ( )  B_SPLINE_CURVE ( 3, ( #80450, #125365, #26054, #134106 ),
 .UNSPECIFIED., .F., .T. ) 
 B_SPLINE_CURVE_WITH_KNOTS ( ( 4, 4 ),
 ( 5.005968288816745826, 5.074607125596321211 ),
 .UNSPECIFIED. ) 
 CURVE ( )  GEOMETRIC_REPRESENTATION_ITEM ( )  RATIONAL_B_SPLINE_CURVE ( ( 1.000000000000000000, 0.9996074310407767616, 0.9996074310407767616, 1.000000000000000000 ) ) 
 REPRESENTATION_ITEM ( '' )  );
#117896=ADVANCED_FACE ( 'NONE', ( #29879 ), #85688, .F. ) ;
#117897=EDGE_CURVE ( 'NONE', #39448, #136399, #72750, .T. ) ;
#117899=EDGE_LOOP ( 'NONE', ( #28378, #37924, #69162, #129690 ) ) ;
#117901=ORIENTED_EDGE ( 'NONE', *, *, #111222, .F. ) ;
#117902=ADVANCED_FACE ( 'NONE', ( #95862 ), #130665, .T. ) ;
#117903=ORIENTED_EDGE ( 'NONE', *, *, #54193, .T. ) ;
#117904=VECTOR ( 'NONE', #123045, 1000.000000000000000 ) ;
#117905=AXIS2_PLACEMENT_3D ( 'NONE', #9640, #65515, #130760 ) ;
#117906=LINE ( 'NONE', #51988, #102280 ) ;
#117907=CARTESIAN_POINT ( 'NONE',  ( 25.01459476339044130, 2.945717840782780428, 4.000000000000000000 ) ) ;
#117912=CARTESIAN_POINT ( 'NONE',  ( 3.183988606268992161, 28.73617430169789699, 5.000000000000000000 ) ) ;
#117913=DIRECTION ( 'NONE',  ( -0.7071067811865486830, 0.7071067811865464625, 0.000000000000000000 ) ) ;
#117914=DIRECTION ( 'NONE',  ( 1.000000000000000000, -0.000000000000000000, -0.000000000000000000 ) ) ;
#117916=ADVANCED_FACE ( 'NONE', ( #83592 ), #31337, .F. ) ;
#117917=LINE ( 'NONE', #41110, #130172 ) ;
#117919=AXIS2_PLACEMENT_3D ( 'NONE', #71914, #6567, #16027 ) ;
#117920=DIRECTION ( 'NONE',  ( -0.7071067811865486830, -0.7071067811865464625, 0.000000000000000000 ) ) ;
#117921=CARTESIAN_POINT ( 'NONE',  ( 20.29289321881332242, -9.740707523384179112, 5.000000000000000000 ) ) ;
#117922=VECTOR ( 'NONE', #143173, 999.9999999999998863 ) ;
#117923=ORIENTED_EDGE ( 'NONE', *, *, #45314, .F. ) ;
#117924=LINE ( 'NONE', #62900, #59806 ) ;
#117925=VERTEX_POINT ( 'NONE', #42227 ) ;
#117926=LINE ( 'NONE', #62902, #6645 ) ;
#117927=ORIENTED_EDGE ( 'NONE', *, *, #33758, .F. ) ;
#117929=VECTOR ( 'NONE', #19815, 1000.000000000000000 ) ;
#117930=EDGE_CURVE ( 'NONE', #11288, #123567, #30636, .T. ) ;
#117932=ORIENTED_EDGE ( 'NONE', *, *, #42033, .T. ) ;
#117933=LINE ( 'NONE', #40438, #99838 ) ;
#117934=DIRECTION ( 'NONE',  ( 0.7071067811865486830, -0.7071067811865464625, -0.000000000000000000 ) ) ;
#117937=CARTESIAN_POINT ( 'NONE',  ( -4.499999999999955591, 10.08746187583914278, 4.000000000000000000 ) ) ;
#117938=EDGE_CURVE ( 'NONE', #18953, #27906, #127806, .T. ) ;
#117939=LINE ( 'NONE', #119381, #30167 ) ;
#117940=VECTOR ( 'NONE', #79762, 999.9999999999998863 ) ;
#117941=CARTESIAN_POINT ( 'NONE',  ( -21.48921356237309155, -27.52281430457070499, 5.000000000000000000 ) ) ;
#117942=CARTESIAN_POINT ( 'NONE',  ( -11.54016161050252975, 18.75929247661552424, 8.305906642995461553 ) ) ;
#117944=FACE_OUTER_BOUND ( 'NONE', #138870, .T. ) ;
#117945=ADVANCED_FACE ( 'NONE', ( #6667 ), #62547, .F. ) ;
#117947=CARTESIAN_POINT ( 'NONE',  ( -39.18398860626899705, 28.73617430169814568, 5.000000000000000000 ) ) ;
#117949=ADVANCED_FACE ( 'NONE', ( #73419 ), #107447, .F. ) ;
#117950=ORIENTED_EDGE ( 'NONE', *, *, #101886, .F. ) ;
#117951=VERTEX_POINT ( 'NONE', #51666 ) ;
#117952=ORIENTED_EDGE ( 'NONE', *, *, #46227, .F. ) ;
#117953=ADVANCED_FACE ( 'NONE', ( #53058 ), #140779, .F. ) ;
#117958=CARTESIAN_POINT ( 'NONE',  ( 14.99999999999989519, -9.033600742197645417, 5.000000000000000000 ) ) ;
#117959=ORIENTED_EDGE ( 'NONE', *, *, #97316, .T. ) ;
#117961=CARTESIAN_POINT ( 'NONE',  ( -32.99451991528749062, 28.92564299267960948, 4.000000000000000000 ) ) ;
#117962=PLANE ( 'NONE',  #59795 ) ;
#117963=EDGE_CURVE ( 'NONE', #10446, #11839, #63285, .T. ) ;
#117964=LINE ( 'NONE', #86821, #113770 ) ;
#117965=ORIENTED_EDGE ( 'NONE', *, *, #33720, .F. ) ;
#117966=ORIENTED_EDGE ( 'NONE', *, *, #45029, .T. ) ;
#117968=FACE_OUTER_BOUND ( 'NONE', #30638, .T. ) ;
#117969=FACE_OUTER_BOUND ( 'NONE', #60621, .T. ) ;
#117970=LINE ( 'NONE', #7065, #21919 ) ;
#117972=LINE ( 'NONE', #17273, #25405 ) ;
#117973=DIRECTION ( 'NONE',  ( -0.7071067811865487940, 0.7071067811865463515, -0.000000000000000000 ) ) ;
#117974=CARTESIAN_POINT ( 'NONE',  ( 63.18398860626900415, 28.73617430169831621, 5.000000000000000000 ) ) ;
#117976=ADVANCED_FACE ( 'NONE', ( #119040 ), #63966, .T. ) ;
#117979=VERTEX_POINT ( 'NONE', #78408 ) ;
#117980=CARTESIAN_POINT ( 'NONE',  ( 15.09667064187396335, -2.240707523384257716, 15.26439735382755636 ) ) ;
#117981=VECTOR ( 'NONE', #111006, 1000.000000000000000 ) ;
#117982=VECTOR ( 'NONE', #136721, 1000.000000000000000 ) ;
#117983=VECTOR ( 'NONE', #36355, 1000.000000000000000 ) ;
#117984=DIRECTION ( 'NONE',  ( 1.000000000000000000, -0.000000000000000000, -0.000000000000000000 ) ) ;
#117985=ORIENTED_EDGE ( 'NONE', *, *, #20302, .F. ) ;
#117986=VECTOR ( 'NONE', #76444, 999.9999999999998863 ) ;
#117987=LINE ( 'NONE', #7081, #136277 ) ;
#117990=ADVANCED_FACE ( 'NONE', ( #65417 ), #136164, .F. ) ;
#117991=CARTESIAN_POINT ( 'NONE',  ( 25.49999999999982947, -13.91253812416061031, 4.000000000000000000 ) ) ;
#117994=FACE_OUTER_BOUND ( 'NONE', #87822, .T. ) ;
#117995=VERTEX_POINT ( 'NONE', #10270 ) ;
#117997=EDGE_CURVE ( 'NONE', #83817, #65537, #121877, .T. ) ;
#117999=FACE_OUTER_BOUND ( 'NONE', #29142, .T. ) ;
#118000=VECTOR ( 'NONE', #47806, 1000.000000000000000 ) ;
#118001=CARTESIAN_POINT ( 'NONE',  ( -65.99451991528749772, 28.92564299267984396, 4.000000000000000000 ) ) ;
#118002=DIRECTION ( 'NONE',  ( 0.6830127018922180770, -0.6830127018922204085, -0.2588190451025213501 ) ) ;
#118003=CARTESIAN_POINT ( 'NONE',  ( -32.67183060077623225, -18.74070752338409207, 4.000000000000000000 ) ) ;
#118004=DIRECTION ( 'NONE',  ( 0.3543493200069163240, -0.000000000000000000, -0.9351131265310288487 ) ) ;
#118007=VECTOR ( 'NONE', #4402, 1000.000000000000000 ) ;
#118008=VECTOR ( 'NONE', #79614, 1000.000000000000114 ) ;
#118009=FACE_OUTER_BOUND ( 'NONE', #4127, .T. ) ;
#118010=DIRECTION ( 'NONE',  ( 0.7071067811865487940, -0.7071067811865463515, 0.000000000000000000 ) ) ;
#118011=ORIENTED_EDGE ( 'NONE', *, *, #35527, .F. ) ;
#118012=ORIENTED_EDGE ( 'NONE', *, *, #47383, .F. ) ;
#118015=EDGE_CURVE ( 'NONE', #82440, #67593, #98710, .T. ) ;
#118016=EDGE_LOOP ( 'NONE', ( #71230, #29355, #78377 ) ) ;
#118017=DIRECTION ( 'NONE',  ( -0.3543493200069162685, -0.000000000000000000, -0.9351131265310288487 ) ) ;
#118019=FACE_OUTER_BOUND ( 'NONE', #83779, .T. ) ;
#118022=AXIS2_PLACEMENT_3D ( 'NONE', #92024, #14476, #80469 ) ;
#118023=LINE ( 'NONE', #19465, #132180 ) ;
#118024=LINE ( 'NONE', #7120, #71924 ) ;
#118025=LINE ( 'NONE', #19467, #81288 ) ;
#118026=EDGE_CURVE ( 'NONE', #87748, #71142, #122604, .T. ) ;
#118028=AXIS2_PLACEMENT_3D ( 'NONE', #5345, #72101, #128580 ) ;
#118030=CARTESIAN_POINT ( 'NONE',  ( 0.000000000000000000, 0.000000000000000000, 5.000000000000000000 ) ) ;
#118032=LINE ( 'NONE', #75304, #292 ) ;
#118034=FACE_OUTER_BOUND ( 'NONE', #85155, .T. ) ;
#118035=DIRECTION ( 'NONE',  ( 0.7071067811865487940, 0.7071067811865463515, 0.000000000000000000 ) ) ;
#118036=PLANE ( 'NONE',  #45258 ) ;
#118037=CARTESIAN_POINT ( 'NONE',  ( 20.99451991528748707, 28.92564299267952777, 4.000000000000000000 ) ) ;
#118039=ORIENTED_EDGE ( 'NONE', *, *, #130, .T. ) ;
#118043=ORIENTED_EDGE ( 'NONE', *, *, #131043, .T. ) ;
#118045=CARTESIAN_POINT ( 'NONE',  ( 19.49999999999986144, 11.52377502935404685, -1.522421517564130022 ) ) ;
#118046=VERTEX_POINT ( 'NONE', #47774 ) ;
#118047=CARTESIAN_POINT ( 'NONE',  ( 54.18398860626899705, 28.73617430169825226, 5.000000000000000000 ) ) ;
#118048=DIRECTION ( 'NONE',  ( -0.7071067811865486830, 0.7071067811865464625, 0.000000000000000000 ) ) ;
#118050=EDGE_LOOP ( 'NONE', ( #117391, #66202, #64538 ) ) ;
#118051=DIRECTION ( 'NONE',  ( 0.7071067811865487940, 0.7071067811865463515, -0.000000000000000000 ) ) ;
#118054=CARTESIAN_POINT ( 'NONE',  ( -44.99451991528749772, 28.92564299267969474, 4.000000000000000000 ) ) ;
#118056=DIRECTION ( 'NONE',  ( -0.000000000000000000, -0.000000000000000000, 1.000000000000000000 ) ) ;
#118057=EDGE_CURVE ( 'NONE', #79175, #104658, #44379, .T. ) ;
#118059=EDGE_LOOP ( 'NONE', ( #50835, #133113, #131336, #133888 ) ) ;
#118061=DIRECTION ( 'NONE',  ( 0.3543493200069162685, -0.000000000000000000, -0.9351131265310288487 ) ) ;
#118062=EDGE_CURVE ( 'NONE', #35602, #22434, #89279, .T. ) ;
#118063=CARTESIAN_POINT ( 'NONE',  ( 21.32816939922339117, 20.25929247661551358, 4.000000000000000000 ) ) ;
#118065=VECTOR ( 'NONE', #2658, 999.9999999999998863 ) ;
#118067=ADVANCED_FACE ( 'NONE', ( #12415 ), #33501, .F. ) ;
#118068=EDGE_CURVE ( 'NONE', #24388, #116780, #98019, .T. ) ;
#118069=ADVANCED_FACE ( 'NONE', ( #132088 ), #110287, .F. ) ;
#118070=ORIENTED_EDGE ( 'NONE', *, *, #50693, .T. ) ;
#118072=DIRECTION ( 'NONE',  ( -0.7071067811865486830, -0.7071067811865464625, 0.000000000000000000 ) ) ;
#118073=EDGE_CURVE ( 'NONE', #109228, #49213, #133505, .T. ) ;
#118074=ORIENTED_EDGE ( 'NONE', *, *, #93318, .T. ) ;
#118075=ORIENTED_EDGE ( 'NONE', *, *, #61898, .F. ) ;
#118076=EDGE_CURVE ( 'NONE', #6847, #129216, #32781, .T. ) ;
#118077=EDGE_CURVE ( 'NONE', #68720, #99304, #67556, .T. ) ;
#118078=VECTOR ( 'NONE', #143314, 1000.000000000000227 ) ;
#118079=PLANE ( 'NONE',  #11844 ) ;
#118081=VERTEX_POINT ( 'NONE', #10963 ) ;
#118082=LINE ( 'NONE', #116693, #46040 ) ;
#118083=VECTOR ( 'NONE', #98826, 1000.000000000000000 ) ;
#118084=LINE ( 'NONE', #107238, #66390 ) ;
#118085=LINE ( 'NONE', #52843, #39085 ) ;
#118086=AXIS2_PLACEMENT_3D ( 'NONE', #111964, #36526, #46750 ) ;
#118088=AXIS2_PLACEMENT_3D ( 'NONE', #13674, #34054, #57967 ) ;
#118090=ORIENTED_EDGE ( 'NONE', *, *, #14525, .T. ) ;
#118091=VECTOR ( 'NONE', #28840, 1000.000000000000000 ) ;
#118092=EDGE_CURVE ( 'NONE', #73824, #91475, #55228, .T. ) ;
#118093=DIRECTION ( 'NONE',  ( 0.7071067811865487940, 0.7071067811865463515, 0.000000000000000000 ) ) ;
#118094=DIRECTION ( 'NONE',  ( -0.7071067811865486830, -0.7071067811865464625, -0.000000000000000000 ) ) ;
#118095=EDGE_LOOP ( 'NONE', ( #14327, #75819, #18998, #105909 ) ) ;
#118096=DIRECTION ( 'NONE',  ( 0.6830127018922180770, -0.6830127018922204085, -0.2588190451025213501 ) ) ;
#118098=LINE ( 'NONE', #73225, #5191 ) ;
#118099=ORIENTED_EDGE ( 'NONE', *, *, #75264, .F. ) ;
#118100=CARTESIAN_POINT ( 'NONE',  ( 14.67183060077637613, 8.259292476615641476, 4.000000000000000000 ) ) ;
#118101=ORIENTED_EDGE ( 'NONE', *, *, #17190, .T. ) ;
#118102=ORIENTED_EDGE ( 'NONE', *, *, #130455, .F. ) ;
#118103=AXIS2_PLACEMENT_3D ( 'NONE', #2873, #47171, #124664 ) ;
#118104=ADVANCED_FACE ( 'NONE', ( #132818 ), #88586, .F. ) ;
#118105=ORIENTED_EDGE ( 'NONE', *, *, #91788, .T. ) ;
#118106=DIRECTION ( 'NONE',  ( 0.6830127018922180770, -0.6830127018922204085, -0.2588190451025213501 ) ) ;
#118107=CARTESIAN_POINT ( 'NONE',  ( 31.49999999999977263, 22.22500000000000142, 4.362957392718809224 ) ) ;
#118108=DIRECTION ( 'NONE',  ( -0.000000000000000000, 0.3543493200069153248, 0.9351131265310291818 ) ) ;
#118109=DIRECTION ( 'NONE',  ( 0.6830127018922181881, 0.6830127018922202975, -0.2588190451025214056 ) ) ;
#118111=DIRECTION ( 'NONE',  ( -0.7071067811865486830, 0.7071067811865464625, 0.000000000000000000 ) ) ;
#118112=CARTESIAN_POINT ( 'NONE',  ( -14.99999999999989519, -5.527737879153202805, -7.983877177622336951 ) ) ;
#118113=AXIS2_PLACEMENT_3D ( 'NONE', #34103, #122498, #23173 ) ;
#118115=DIRECTION ( 'NONE',  ( 0.7071067811865487940, 0.7071067811865463515, 0.000000000000000000 ) ) ;
#118116=AXIS2_PLACEMENT_3D ( 'NONE', #99519, #56083, #68385 ) ;
#118117=DIRECTION ( 'NONE',  ( -0.7071067811865486830, -0.7071067811865464625, 0.000000000000000000 ) ) ;
#118118=VECTOR ( 'NONE', #111911, 1000.000000000000000 ) ;
#118119=LINE ( 'NONE', #84813, #140899 ) ;
#118124=ORIENTED_EDGE ( 'NONE', *, *, #137841, .T. ) ;
#118125=VERTEX_POINT ( 'NONE', #83967 ) ;
#118126=ORIENTED_EDGE ( 'NONE', *, *, #17022, .F. ) ;
#118129=AXIS2_PLACEMENT_3D ( 'NONE', #11926, #56215, #56913 ) ;
#118130=ADVANCED_FACE ( 'NONE', ( #95505 ), #5624, .F. ) ;
#118131=ORIENTED_EDGE ( 'NONE', *, *, #13852, .T. ) ;
#118132=CARTESIAN_POINT ( 'NONE',  ( -13.08100000000000307, 3.174999999999997158, 4.000000000000000000 ) ) ;
#118133=CARTESIAN_POINT ( 'NONE',  ( 12.29177708983039707, -15.74070752338412049, 19.73771281079100604 ) ) ;
#118134=AXIS2_PLACEMENT_3D ( 'NONE', #7799, #96931, #31025 ) ;
#118135=DIRECTION ( 'NONE',  ( 0.7071067811865487940, 0.7071067811865463515, -0.000000000000000000 ) ) ;
#118137=CARTESIAN_POINT ( 'NONE',  ( 13.49999999999990408, 22.01701374228156283, 2.453858888625600532 ) ) ;
#118138=ORIENTED_EDGE ( 'NONE', *, *, #126818, .F. ) ;
#118139=EDGE_CURVE ( 'NONE', #24994, #56274, #38999, .T. ) ;
#118140=CARTESIAN_POINT ( 'NONE',  ( -69.48921356237309510, -27.52281430457103895, 5.000000000000000000 ) ) ;
#118141=PLANE ( 'NONE',  #89004 ) ;
#118143=EDGE_LOOP ( 'NONE', ( #117950, #18472, #39177, #30391 ) ) ;
#118145=CARTESIAN_POINT ( 'NONE',  ( -34.92500000000001137, 22.22500000000000142, 4.000000000000000000 ) ) ;
#118147=EDGE_CURVE ( 'NONE', #19029, #15867, #16505, .T. ) ;
#118148=CARTESIAN_POINT ( 'NONE',  ( -28.62823445044367432, -8.240707523384200428, 11.38925528200759096 ) ) ;
#118150=ORIENTED_EDGE ( 'NONE', *, *, #84535, .F. ) ;
#118152=VECTOR ( 'NONE', #53532, 999.9999999999998863 ) ;
#118153=ORIENTED_EDGE ( 'NONE', *, *, #56529, .F. ) ;
#118154=CARTESIAN_POINT ( 'NONE',  ( -20.20666063542138957, 21.75929247661549226, 4.998822639870715179 ) ) ;
#118156=LINE ( 'NONE', #19584, #102513 ) ;
#118157=CARTESIAN_POINT ( 'NONE',  ( 18.48921356237309510, -27.52281430457068367, 5.000000000000000000 ) ) ;
#118159=CARTESIAN_POINT ( 'NONE',  ( 10.49999999999992717, -7.533600742197660516, 5.000000000000000000 ) ) ;
#118160=ADVANCED_FACE ( 'NONE', ( #49185 ), #92640, .F. ) ;
#118161=LINE ( 'NONE', #97876, #113782 ) ;
#118162=CARTESIAN_POINT ( 'NONE',  ( -8.999999999999934275, -8.731860332648849976, -2.120594902707559015 ) ) ;
#118164=LINE ( 'NONE', #18873, #123075 ) ;
#118166=DIRECTION ( 'NONE',  ( -0.000000000000000000, -0.3543493200069152693, 0.9351131265310292928 ) ) ;
#118167=ORIENTED_EDGE ( 'NONE', *, *, #24868, .F. ) ;
#118168=CARTESIAN_POINT ( 'NONE',  ( 28.49999999999981171, 5.696342897626538893, -7.587980461218336359 ) ) ;
#118169=VERTEX_POINT ( 'NONE', #127424 ) ;
#118170=EDGE_CURVE ( 'NONE', #23219, #87976, #17241, .T. ) ;
#118171=EDGE_LOOP ( 'NONE', ( #94281, #121144, #78971 ) ) ;
#118174=CARTESIAN_POINT ( 'NONE',  ( 0.000000000000000000, 0.000000000000000000, 5.000000000000000000 ) ) ;
#118175=VECTOR ( 'NONE', #29248, 1000.000000000000000 ) ;
#118176=VERTEX_POINT ( 'NONE', #38292 ) ;
#118177=DIRECTION ( 'NONE',  ( -0.7071067811865486830, 0.7071067811865463515, 0.000000000000000000 ) ) ;
#118179=CARTESIAN_POINT ( 'NONE',  ( 3.299744871391591339, -27.71228299555208352, 4.000000000000000000 ) ) ;
#118180=EDGE_CURVE ( 'NONE', #121472, #14718, #103514, .T. ) ;
#118182=CARTESIAN_POINT ( 'NONE',  ( 7.589909354801631203, 9.759292476615618384, 11.28811694763780515 ) ) ;
#118184=CARTESIAN_POINT ( 'NONE',  ( 17.51078643762690845, -27.52281430457043143, 5.000000000000000000 ) ) ;
#118185=LINE ( 'NONE', #18896, #65726 ) ;
#118186=CARTESIAN_POINT ( 'NONE',  ( -39.48921356237310221, -27.52281430457082934, 5.000000000000000000 ) ) ;
#118187=CARTESIAN_POINT ( 'NONE',  ( -51.18398860626899705, 28.73617430169823095, 5.000000000000000000 ) ) ;
#118189=CARTESIAN_POINT ( 'NONE',  ( -18.46160355370559003, -9.740707523384180888, 17.74957260769606648 ) ) ;
#118190=VECTOR ( 'NONE', #10255, 1000.000000000000000 ) ;
#118191=DIRECTION ( 'NONE',  ( 0.3543493200069162685, -0.000000000000000000, -0.9351131265310288487 ) ) ;
#118193=VERTEX_POINT ( 'NONE', #37587 ) ;
#118194=EDGE_CURVE ( 'NONE', #89301, #69618, #81829, .T. ) ;
#118195=VERTEX_POINT ( 'NONE', #85335 ) ;
#118196=ORIENTED_EDGE ( 'NONE', *, *, #118026, .F. ) ;
#118197=VECTOR ( 'NONE', #36991, 1000.000000000000114 ) ;
#118199=VECTOR ( 'NONE', #135246, 1000.000000000000000 ) ;
#118201=ORIENTED_EDGE ( 'NONE', *, *, #31396, .T. ) ;
#118202=ORIENTED_EDGE ( 'NONE', *, *, #30698, .T. ) ;
#118203=EDGE_LOOP ( 'NONE', ( #118707, #73990, #74708, #81756 ) ) ;
#118204=CARTESIAN_POINT ( 'NONE',  ( 45.18398860626900415, 28.73617430169818832, 5.000000000000000000 ) ) ;
#118206=VECTOR ( 'NONE', #6700, 1000.000000000000227 ) ;
#118207=VECTOR ( 'NONE', #30878, 1000.000000000000000 ) ;
#118208=VECTOR ( 'NONE', #90377, 1000.000000000000000 ) ;
#118209=AXIS2_PLACEMENT_3D ( 'NONE', #62230, #111226, #45319 ) ;
#118210=EDGE_LOOP ( 'NONE', ( #98746, #64670, #113522, #2339 ) ) ;
#118213=CARTESIAN_POINT ( 'NONE',  ( -3.707106781186510602, -12.74070752338415602, 5.000000000000000000 ) ) ;
#118214=CARTESIAN_POINT ( 'NONE',  ( -72.48921356237309510, -27.52281430457106026, 5.000000000000000000 ) ) ;
#118215=LINE ( 'NONE', #106617, #11806 ) ;
#118218=EDGE_CURVE ( 'NONE', #27002, #51146, #20078, .T. ) ;
#118220=CARTESIAN_POINT ( 'NONE',  ( -24.70701326429287903, -21.74070752338406365, 4.999753212805221558 ) ) ;
#118221=CARTESIAN_POINT ( 'NONE',  ( 27.79289321881326558, 6.759292476615653023, 5.000000000000000000 ) ) ;
#118223=FACE_OUTER_BOUND ( 'NONE', #42230, .T. ) ;
#118224=CARTESIAN_POINT ( 'NONE',  ( 45.48921356237309510, -27.52281430457087197, 5.000000000000000000 ) ) ;
#118226=LINE ( 'NONE', #74040, #141778 ) ;
#118227=ORIENTED_EDGE ( 'NONE', *, *, #245, .F. ) ;
#118228=VERTEX_POINT ( 'NONE', #109954 ) ;
#118230=VERTEX_POINT ( 'NONE', #52023 ) ;
#118231=AXIS2_PLACEMENT_3D ( 'NONE', #95103, #127763, #27712 ) ;
#118233=VECTOR ( 'NONE', #88093, 1000.000000000000000 ) ;
#118235=CARTESIAN_POINT ( 'NONE',  ( 8.510786437626906675, -27.52281430457049183, 5.000000000000000000 ) ) ;
#118236=DIRECTION ( 'NONE',  ( 0.6830127018922180770, -0.6830127018922204085, -0.2588190451025213501 ) ) ;
#118239=VECTOR ( 'NONE', #3083, 1000.000000000000000 ) ;
#118242=ORIENTED_EDGE ( 'NONE', *, *, #116443, .T. ) ;
#118243=VECTOR ( 'NONE', #35563, 1000.000000000000000 ) ;
#118244=LINE ( 'NONE', #61773, #3873 ) ;
#118245=ADVANCED_FACE ( 'NONE', ( #96902 ), #141148, .T. ) ;
#118246=ORIENTED_EDGE ( 'NONE', *, *, #30443, .T. ) ;
#118247=LINE ( 'NONE', #140046, #53179 ) ;
#118249=CARTESIAN_POINT ( 'NONE',  ( 15.32816939922342669, 11.25929247661561128, 4.000000000000000000 ) ) ;
#118251=CARTESIAN_POINT ( 'NONE',  ( -0.1839886062690032631, 28.73617430169787568, 5.000000000000000000 ) ) ;
#118254=ORIENTED_EDGE ( 'NONE', *, *, #21944, .T. ) ;
#118255=AXIS2_PLACEMENT_3D ( 'NONE', #111987, #58360, #14792 ) ;
#118256=CARTESIAN_POINT ( 'NONE',  ( 0.000000000000000000, 0.000000000000000000, 5.000000000000000000 ) ) ;
#118257=DIRECTION ( 'NONE',  ( 0.7071067811865487940, 0.7071067811865463515, 0.000000000000000000 ) ) ;
#118258=CARTESIAN_POINT ( 'NONE',  ( -34.42500000000001137, 22.22500000000000142, 0.4999999999999995559 ) ) ;
#118260=EDGE_CURVE ( 'NONE', #84967, #33497, #86076, .T. ) ;
#118263=EDGE_CURVE ( 'NONE', #100536, #109228, #63638, .T. ) ;
#118264=VERTEX_POINT ( 'NONE', #142606 ) ;
#118265=CARTESIAN_POINT ( 'NONE',  ( 51.18398860626899705, 28.73617430169823095, 5.000000000000000000 ) ) ;
#118266=EDGE_CURVE ( 'NONE', #53028, #75919, #40450, .T. ) ;
#118267=ORIENTED_EDGE ( 'NONE', *, *, #52842, .T. ) ;
#118268=ORIENTED_EDGE ( 'NONE', *, *, #84339, .T. ) ;
#118270=ORIENTED_EDGE ( 'NONE', *, *, #43389, .T. ) ;
#118271=VECTOR ( 'NONE', #74723, 999.9999999999998863 ) ;
#118273=CARTESIAN_POINT ( 'NONE',  ( -1.499999999999991784, 22.01701374228155572, 2.453858888625634727 ) ) ;
#118275=VERTEX_POINT ( 'NONE', #18639 ) ;
#118277=EDGE_CURVE ( 'NONE', #37506, #71573, #109243, .T. ) ;
#118278=AXIS2_PLACEMENT_3D ( 'NONE', #123736, #80937, #49028 ) ;
#118279=DIRECTION ( 'NONE',  ( 0.000000000000000000, 0.000000000000000000, 1.000000000000000000 ) ) ;
#118282=FACE_BOUND ( 'NONE', #141560, .T. ) ;
#118284=EDGE_CURVE ( 'NONE', #47269, #25807, #20801, .T. ) ;
#118285=CARTESIAN_POINT ( 'NONE',  ( 21.48921356237309155, -27.52281430457070499, 5.000000000000000000 ) ) ;
#118286=LINE ( 'NONE', #8086, #102308 ) ;
#118288=ORIENTED_EDGE ( 'NONE', *, *, #41351, .F. ) ;
#118289=DIRECTION ( 'NONE',  ( 0.7071067811865487940, 0.7071067811865463515, -0.000000000000000000 ) ) ;
#118295=VERTEX_POINT ( 'NONE', #65054 ) ;
#118297=ORIENTED_EDGE ( 'NONE', *, *, #46378, .F. ) ;
#118300=LINE ( 'NONE', #107437, #56596 ) ;
#118301=ORIENTED_EDGE ( 'NONE', *, *, #64950, .T. ) ;
#118303=VECTOR ( 'NONE', #112790, 1000.000000000000000 ) ;
#118304=VECTOR ( 'NONE', #4838, 999.9999999999998863 ) ;
#118305=DIRECTION ( 'NONE',  ( -0.6830127018922180770, -0.6830127018922204085, -0.2588190451025213501 ) ) ;
#118306=FACE_OUTER_BOUND ( 'NONE', #15033, .T. ) ;
#118309=CARTESIAN_POINT ( 'NONE',  ( -34.49999999999975131, -19.53574439159930876, 4.994342998332169437 ) ) ;
#118310=ORIENTED_EDGE ( 'NONE', *, *, #16502, .T. ) ;
#118311=EDGE_CURVE ( 'NONE', #26486, #62201, #76649, .T. ) ;
#118312=VECTOR ( 'NONE', #60837, 1000.000000000000227 ) ;
#118313=VECTOR ( 'NONE', #33040, 999.9999999999998863 ) ;
#118314=AXIS2_PLACEMENT_3D ( 'NONE', #54751, #43159, #88810 ) ;
#118315=ORIENTED_EDGE ( 'NONE', *, *, #112411, .T. ) ;
#118316=AXIS2_PLACEMENT_3D ( 'NONE', #6413, #18020, #104334 ) ;
#118318=CARTESIAN_POINT ( 'NONE',  ( -27.18398860626900060, 28.73617430169806042, 5.000000000000000000 ) ) ;
#118319=VERTEX_POINT ( 'NONE', #98385 ) ;
#118320=VECTOR ( 'NONE', #116213, 1000.000000000000000 ) ;
#118321=ORIENTED_EDGE ( 'NONE', *, *, #128574, .F. ) ;
#118324=CARTESIAN_POINT ( 'NONE',  ( 16.17183060077635659, -11.24070752338416668, 4.000000000000000000 ) ) ;
#118325=ORIENTED_EDGE ( 'NONE', *, *, #73757, .T. ) ;
#118326=VECTOR ( 'NONE', #125769, 1000.000000000000114 ) ;
#118327=FACE_OUTER_BOUND ( 'NONE', #108742, .T. ) ;
#118328=EDGE_CURVE ( 'NONE', #55786, #89397, #7773, .T. ) ;
#118329=DIRECTION ( 'NONE',  ( 0.7071067811865487940, 0.7071067811865463515, -0.000000000000000000 ) ) ;
#118331=CARTESIAN_POINT ( 'NONE',  ( 28.49999999999980815, -4.796895815300988630, -3.611700055028616685 ) ) ;
#118332=VERTEX_POINT ( 'NONE', #41133 ) ;
#118334=VECTOR ( 'NONE', #51109, 999.9999999999998863 ) ;
#118335=CARTESIAN_POINT ( 'NONE',  ( -8.381615093979984721, -2.240707523384260824, 13.37739548510241328 ) ) ;
#118336=EDGE_CURVE ( 'NONE', #56372, #11859, #30254, .T. ) ;
#118337=PLANE ( 'NONE',  #118987 ) ;
#118338=LINE ( 'NONE', #19040, #98075 ) ;
#118339=ORIENTED_EDGE ( 'NONE', *, *, #130567, .T. ) ;
#118341=ORIENTED_EDGE ( 'NONE', *, *, #133692, .F. ) ;
#118342=PLANE ( 'NONE',  #121362 ) ;
#118344=CARTESIAN_POINT ( 'NONE',  ( 21.48921356237309155, -27.52281430457070499, 5.000000000000000000 ) ) ;
#118345=VERTEX_POINT ( 'NONE', #133169 ) ;
#118346=VECTOR ( 'NONE', #2366, 999.9999999999998863 ) ;
#118348=VECTOR ( 'NONE', #33324, 1000.000000000000227 ) ;
#118352=ORIENTED_EDGE ( 'NONE', *, *, #28267, .F. ) ;
#118353=DIRECTION ( 'NONE',  ( -0.7071067811865486830, -0.7071067811865464625, 0.000000000000000000 ) ) ;
#118355=CARTESIAN_POINT ( 'NONE',  ( -27.48921356237309155, -27.52281430457074762, 5.000000000000000000 ) ) ;
#118357=FACE_OUTER_BOUND ( 'NONE', #92255, .T. ) ;
#118358=VERTEX_POINT ( 'NONE', #12063 ) ;
#118360=AXIS2_PLACEMENT_3D ( 'NONE', #36220, #23154, #100751 ) ;
#118362=DIRECTION ( 'NONE',  ( -0.6830127018922181881, 0.6830127018922202975, -0.2588190451025214056 ) ) ;
#118363=CARTESIAN_POINT ( 'NONE',  ( 1.499999999999997780, -20.94781430457061333, 5.000000000000000000 ) ) ;
#118366=VECTOR ( 'NONE', #59319, 1000.000000000000000 ) ;
#118367=CARTESIAN_POINT ( 'NONE',  ( -17.99999999999987566, -13.97847968911261951, -0.1324546996127216603 ) ) ;
#118368=DIRECTION ( 'NONE',  ( 0.7071067811865487940, 0.7071067811865463515, -0.000000000000000000 ) ) ;
#118370=DIRECTION ( 'NONE',  ( 0.3543493200069163240, -0.000000000000000000, -0.9351131265310288487 ) ) ;
#118371=CARTESIAN_POINT ( 'NONE',  ( -48.48921356237309510, -27.52281430457089328, 5.000000000000000000 ) ) ;
#118373=CARTESIAN_POINT ( 'NONE',  ( 17.99999999999987566, 18.08204922493374767, 0.9627537363044456065 ) ) ;
#118375=DIRECTION ( 'NONE',  ( 0.7071067811865486830, -0.7071067811865464625, -0.000000000000000000 ) ) ;
#118377=CARTESIAN_POINT ( 'NONE',  ( 32.01088028653925477, -22.02621442084247860, 4.990779571109224655 ) ) ;
#118378=EDGE_LOOP ( 'NONE', ( #29443, #81343, #4642, #132389 ) ) ;
#118379=DIRECTION ( 'NONE',  ( 0.6830127018922180770, -0.6830127018922204085, -0.2588190451025213501 ) ) ;
#118380=EDGE_CURVE ( 'NONE', #69099, #50102, #88222, .T. ) ;
#118381=VERTEX_POINT ( 'NONE', #110642 ) ;
#118382=VERTEX_POINT ( 'NONE', #132474 ) ;
#118383=VECTOR ( 'NONE', #126227, 1000.000000000000000 ) ;
#118384=CARTESIAN_POINT ( 'NONE',  ( 5.994519915287488843, 28.92564299267942118, 4.000000000000000000 ) ) ;
#118385=CARTESIAN_POINT ( 'NONE',  ( 32.29298673570672662, -21.74070752338405654, 4.999753212805222446 ) ) ;
#118386=EDGE_LOOP ( 'NONE', ( #47615, #131842, #123894, #72350 ) ) ;
#118387=DIRECTION ( 'NONE',  ( -0.6830127018922180770, -0.6830127018922204085, -0.2588190451025213501 ) ) ;
#118388=CARTESIAN_POINT ( 'NONE',  ( 12.70710678118645731, 8.259292476615629042, 5.000000000000000000 ) ) ;
#118389=CARTESIAN_POINT ( 'NONE',  ( -7.499999999999944045, -9.462702396501018853, -9.474982329943495429 ) ) ;
#118390=EDGE_CURVE ( 'NONE', #41017, #100429, #33164, .T. ) ;
#118391=CARTESIAN_POINT ( 'NONE',  ( 6.489213562373093325, -27.52281430457059841, 5.000000000000000000 ) ) ;
#118392=CARTESIAN_POINT ( 'NONE',  ( 42.48921356237308800, -27.52281430457085065, 5.000000000000000000 ) ) ;
#118393=ORIENTED_EDGE ( 'NONE', *, *, #1908, .T. ) ;
#118394=EDGE_CURVE ( 'NONE', #19799, #68975, #121539, .T. ) ;
#118396=CARTESIAN_POINT ( 'NONE',  ( -8.816011393731004731, 28.73617430169781173, 5.000000000000000000 ) ) ;
#118397=CARTESIAN_POINT ( 'NONE',  ( 5.700255128608413102, -27.71228299555201957, 4.000000000000000000 ) ) ;
#118399=CARTESIAN_POINT ( 'NONE',  ( 8.671830600776408104, -12.74070752338415602, 4.000000000000000000 ) ) ;
#118401=CARTESIAN_POINT ( 'NONE',  ( 34.42499999999998295, 5.977185695429338530, 5.000000000000000000 ) ) ;
#118403=CARTESIAN_POINT ( 'NONE',  ( 12.79333936457838483, 21.75929247661549937, 4.998822639870715179 ) ) ;
#118405=VERTEX_POINT ( 'NONE', #100529 ) ;
#118407=LINE ( 'NONE', #38730, #33161 ) ;
#118409=LINE ( 'NONE', #52444, #120082 ) ;
#118410=ORIENTED_EDGE ( 'NONE', *, *, #86020, .F. ) ;
#118412=ADVANCED_FACE ( 'NONE', ( #24380 ), #13469, .F. ) ;
#118414=VECTOR ( 'NONE', #99585, 999.9999999999998863 ) ;
#118415=AXIS2_PLACEMENT_3D ( 'NONE', #47565, #14875, #135268 ) ;
#118417=VERTEX_POINT ( 'NONE', #80224 ) ;
#118418=PLANE ( 'NONE',  #47936 ) ;
#118419=ORIENTED_EDGE ( 'NONE', *, *, #84594, .F. ) ;
#118420=VECTOR ( 'NONE', #61387, 1000.000000000000000 ) ;
#118422=AXIS2_PLACEMENT_3D ( 'NONE', #66544, #108562, #20151 ) ;
#118424=VECTOR ( 'NONE', #17861, 1000.000000000000000 ) ;
#118426=VECTOR ( 'NONE', #115278, 1000.000000000000000 ) ;
#118427=CARTESIAN_POINT ( 'NONE',  ( -34.92500000000001137, 6.324594729295654361, 11.02525794543158888 ) ) ;
#118428=CARTESIAN_POINT ( 'NONE',  ( 24.32816939922335919, -18.74070752338409562, 4.000000000000000000 ) ) ;
#118429=ORIENTED_EDGE ( 'NONE', *, *, #63136, .F. ) ;
#118431=CARTESIAN_POINT ( 'NONE',  ( 51.48921356237309510, -27.52281430457091460, 5.000000000000000000 ) ) ;
#118432=ORIENTED_EDGE ( 'NONE', *, *, #23653, .T. ) ;
#118434=LINE ( 'NONE', #19135, #61678 ) ;
#118435=PLANE ( 'NONE',  #137455 ) ;
#118437=DIRECTION ( 'NONE',  ( 0.3543493200069162685, -0.000000000000000000, -0.9351131265310288487 ) ) ;
#118438=CARTESIAN_POINT ( 'NONE',  ( -11.52663903635778020, -5.240707523384218192, 16.25846745537492666 ) ) ;
#118439=EDGE_LOOP ( 'NONE', ( #77736, #64430, #61329, #79982 ) ) ;
#118441=ORIENTED_EDGE ( 'NONE', *, *, #67901, .T. ) ;
#118442=LINE ( 'NONE', #7530, #128684 ) ;
#118444=EDGE_CURVE ( 'NONE', #130332, #132699, #91094, .T. ) ;
#118445=CARTESIAN_POINT ( 'NONE',  ( -34.92500000000001137, -11.33753812416089346, 4.000000000000000000 ) ) ;
#118446=DIRECTION ( 'NONE',  ( -0.7071067811865487940, 0.7071067811865463515, -0.000000000000000000 ) ) ;
#118447=ORIENTED_EDGE ( 'NONE', *, *, #108662, .T. ) ;
#118448=ORIENTED_EDGE ( 'NONE', *, *, #26217, .F. ) ;
#118449=LINE ( 'NONE', #130800, #39981 ) ;
#118450=LINE ( 'NONE', #19153, #63003 ) ;
#118451=VERTEX_POINT ( 'NONE', #88952 ) ;
#118452=ADVANCED_FACE ( 'NONE', ( #133860 ), #33853, .T. ) ;
#118453=EDGE_CURVE ( 'NONE', #88279, #105080, #34553, .T. ) ;
#118454=ORIENTED_EDGE ( 'NONE', *, *, #17869, .T. ) ;
#118455=VECTOR ( 'NONE', #4643, 999.9999999999998863 ) ;
#118459=CARTESIAN_POINT ( 'NONE',  ( -8.109179343494679060, 22.22500000000000142, -5.161516874765829321 ) ) ;
#118460=DIRECTION ( 'NONE',  ( -0.7071067811865487940, 0.7071067811865463515, 0.000000000000000000 ) ) ;
#118462=DIRECTION ( 'NONE',  ( -0.6830127018922181881, 0.6830127018922202975, -0.2588190451025214056 ) ) ;
#118463=ADVANCED_FACE ( 'NONE', ( #72933 ), #94615, .F. ) ;
#118464=FACE_BOUND ( 'NONE', #91391, .T. ) ;
#118465=EDGE_CURVE ( 'NONE', #106952, #5802, #114243, .T. ) ;
#118467=FACE_OUTER_BOUND ( 'NONE', #48206, .T. ) ;
#118469=DIRECTION ( 'NONE',  ( 0.7071067811865487940, -0.7071067811865463515, 0.000000000000000000 ) ) ;
#118471=VECTOR ( 'NONE', #78571, 1000.000000000000000 ) ;
#118472=DIRECTION ( 'NONE',  ( 0.7071067811865486830, -0.7071067811865464625, -0.000000000000000000 ) ) ;
#118474=EDGE_CURVE ( 'NONE', #123094, #391, #117081, .T. ) ;
#118475=VERTEX_POINT ( 'NONE', #70772 ) ;
#118476=ORIENTED_EDGE ( 'NONE', *, *, #83239, .F. ) ;
#118478=ORIENTED_EDGE ( 'NONE', *, *, #90496, .T. ) ;
#118479=DIRECTION ( 'NONE',  ( -0.6830127018922180770, -0.6830127018922204085, -0.2588190451025213501 ) ) ;
#118480=VECTOR ( 'NONE', #23025, 1000.000000000000000 ) ;
#118481=LINE ( 'NONE', #73572, #74850 ) ;
#118483=VECTOR ( 'NONE', #138552, 999.9999999999998863 ) ;
#118484=DIRECTION ( 'NONE',  ( 0.3543493200069162685, -0.000000000000000000, -0.9351131265310288487 ) ) ;
#118485=LINE ( 'NONE', #19880, #32144 ) ;
#118486=CARTESIAN_POINT ( 'NONE',  ( 48.18398860626899705, 28.73617430169820608, 5.000000000000000000 ) ) ;
#118489=CARTESIAN_POINT ( 'NONE',  ( -28.49999999999979039, 0.05218569542916537407, 5.000000000000000000 ) ) ;
#118490=CARTESIAN_POINT ( 'NONE',  ( -30.18398860626900060, 28.73617430169808173, 5.000000000000000000 ) ) ;
#118491=ADVANCED_FACE ( 'NONE', ( #81650 ), #125856, .F. ) ;
#118492=AXIS2_PLACEMENT_3D ( 'NONE', #77735, #100197, #845 ) ;
#118493=ORIENTED_EDGE ( 'NONE', *, *, #132031, .F. ) ;
#118494=CARTESIAN_POINT ( 'NONE',  ( -30.32816939922331656, 17.25929247661554200, 4.000000000000000000 ) ) ;
#118495=CARTESIAN_POINT ( 'NONE',  ( -2.510786437626908008, -27.52281430457053446, 5.000000000000000000 ) ) ;
#118496=ORIENTED_EDGE ( 'NONE', *, *, #122611, .F. ) ;
#118497=VERTEX_POINT ( 'NONE', #71465 ) ;
#118498=LINE ( 'NONE', #140960, #40571 ) ;
#118499=ORIENTED_EDGE ( 'NONE', *, *, #35558, .F. ) ;
#118500=ADVANCED_FACE ( 'NONE', ( #50432 ), #47608, .T. ) ;
#118502=ADVANCED_FACE ( 'NONE', ( #104050 ), #3996, .F. ) ;
#118504=ORIENTED_EDGE ( 'NONE', *, *, #135511, .F. ) ;
#118505=DIRECTION ( 'NONE',  ( -0.7071067811865486830, 0.7071067811865464625, 0.000000000000000000 ) ) ;
#118506=EDGE_CURVE ( 'NONE', #103729, #87648, #17081, .T. ) ;
#118509=ORIENTED_EDGE ( 'NONE', *, *, #18812, .T. ) ;
#118510=DIRECTION ( 'NONE',  ( 0.7071067811865487940, 0.7071067811865463515, -0.000000000000000000 ) ) ;
#118511=ORIENTED_EDGE ( 'NONE', *, *, #72761, .F. ) ;
#118512=CARTESIAN_POINT ( 'NONE',  ( 3.436801032208273821, -12.74070752338415069, 9.898150129686367649 ) ) ;
#118513=CARTESIAN_POINT ( 'NONE',  ( -25.17183060077629619, 9.759292476615618384, 4.000000000000000000 ) ) ;
#118514=VECTOR ( 'NONE', #134448, 1000.000000000000000 ) ;
#118515=AXIS2_PLACEMENT_3D ( 'NONE', #142949, #43638, #88596 ) ;
#118516=LINE ( 'NONE', #49003, #28549 ) ;
#118517=ORIENTED_EDGE ( 'NONE', *, *, #124711, .F. ) ;
#118518=VERTEX_POINT ( 'NONE', #80919 ) ;
#118519=CARTESIAN_POINT ( 'NONE',  ( -17.67183060077634593, 11.25929247661560062, 4.000000000000000000 ) ) ;
#118520=VECTOR ( 'NONE', #96205, 1000.000000000000000 ) ;
#118521=DIRECTION ( 'NONE',  ( -0.6830127018922180770, -0.6830127018922204085, -0.2588190451025214056 ) ) ;
#118522=VECTOR ( 'NONE', #110964, 1000.000000000000000 ) ;
#118523=ORIENTED_EDGE ( 'NONE', *, *, #51554, .T. ) ;
#118525=EDGE_LOOP ( 'NONE', ( #137970, #52072, #56654, #98427 ) ) ;
#118526=EDGE_LOOP ( 'NONE', ( #113843, #128378, #52030, #71482 ) ) ;
#118528=LINE ( 'NONE', #130871, #107314 ) ;
#118529=VECTOR ( 'NONE', #29271, 999.9999999999998863 ) ;
#118532=CARTESIAN_POINT ( 'NONE',  ( 48.48921356237309510, -27.52281430457089328, 5.000000000000000000 ) ) ;
#118533=LINE ( 'NONE', #117787, #42282 ) ;
#118534=CARTESIAN_POINT ( 'NONE',  ( 39.48921356237310221, -27.52281430457082934, 5.000000000000000000 ) ) ;
#118535=CARTESIAN_POINT ( 'NONE',  ( -6.005480084712508493, 28.92564299267933947, 4.000000000000000000 ) ) ;
#118536=ORIENTED_EDGE ( 'NONE', *, *, #78356, .F. ) ;
#118537=LINE ( 'NONE', #19236, #74447 ) ;
#118538=ORIENTED_EDGE ( 'NONE', *, *, #9938, .F. ) ;
#118541=ORIENTED_EDGE ( 'NONE', *, *, #122617, .T. ) ;
#118542=DIRECTION ( 'NONE',  ( -0.7071067811865486830, -0.7071067811865464625, 0.000000000000000000 ) ) ;
#118543=PLANE ( 'NONE',  #130021 ) ;
#118544=ORIENTED_EDGE ( 'NONE', *, *, #142032, .F. ) ;
#118545=VERTEX_POINT ( 'NONE', #115628 ) ;
#118546=EDGE_CURVE ( 'NONE', #122251, #3015, #92756, .T. ) ;
#118547=DIRECTION ( 'NONE',  ( -0.7071067811865486830, 0.7071067811865464625, 0.000000000000000000 ) ) ;
#118550=PLANE ( 'NONE',  #70180 ) ;
#118554=VECTOR ( 'NONE', #126673, 1000.000000000000000 ) ;
#118555=CARTESIAN_POINT ( 'NONE',  ( -12.00548008471251293, 28.92564299267929684, 4.000000000000000000 ) ) ;
#118557=DIRECTION ( 'NONE',  ( -0.000000000000000000, -0.3543493200069152693, 0.9351131265310292928 ) ) ;
#118558=CARTESIAN_POINT ( 'NONE',  ( 25.82816939922335209, 6.759292476615644141, 4.000000000000000000 ) ) ;
#118559=AXIS2_PLACEMENT_3D ( 'NONE', #8636, #52879, #97079 ) ;
#118560=ORIENTED_EDGE ( 'NONE', *, *, #136580, .T. ) ;
#118561=LINE ( 'NONE', #86676, #120487 ) ;
#118562=EDGE_LOOP ( 'NONE', ( #33859, #35432, #118978, #40022 ) ) ;
#118563=DIRECTION ( 'NONE',  ( 0.6830127018922180770, -0.6830127018922204085, -0.2588190451025213501 ) ) ;
#118564=DIRECTION ( 'NONE',  ( -0.000000000000000000, 0.3543493200069153248, 0.9351131265310292928 ) ) ;
#118566=ORIENTED_EDGE ( 'NONE', *, *, #72519, .T. ) ;
#118567=CARTESIAN_POINT ( 'NONE',  ( 0.000000000000000000, 21.72500000000000142, 4.500000000000000888 ) ) ;
#118568=LINE ( 'NONE', #32297, #102096 ) ;
#118569=ORIENTED_EDGE ( 'NONE', *, *, #9064, .F. ) ;
#118570=DIRECTION ( 'NONE',  ( 0.7071067811865486830, -0.7071067811865464625, -0.000000000000000000 ) ) ;
#118572=CARTESIAN_POINT ( 'NONE',  ( -11.90332935812586612, -2.240707523384257716, 15.26439735382749774 ) ) ;
#118573=LINE ( 'NONE', #98952, #137543 ) ;
#118574=EDGE_LOOP ( 'NONE', ( #60883, #56962, #111108, #80762 ) ) ;
#118576=ORIENTED_EDGE ( 'NONE', *, *, #103919, .T. ) ;
#118577=LINE ( 'NONE', #19276, #39753 ) ;
#118578=CARTESIAN_POINT ( 'NONE',  ( 17.99451991528748351, 28.92564299267950645, 4.000000000000000000 ) ) ;
#118581=CARTESIAN_POINT ( 'NONE',  ( -30.48921356237309510, -27.52281430457076894, 5.000000000000000000 ) ) ;
#118583=CARTESIAN_POINT ( 'NONE',  ( 18.47336096364204039, -5.240707523384225297, 16.25846745537499771 ) ) ;
#118584=LINE ( 'NONE', #54784, #140918 ) ;
#118585=VERTEX_POINT ( 'NONE', #4707 ) ;
#118586=ADVANCED_FACE ( 'NONE', ( #49007 ), #93202, .F. ) ;
#118587=DIRECTION ( 'NONE',  ( 0.7071067811865487940, 0.7071067811865463515, 0.000000000000000000 ) ) ;
#118591=VECTOR ( 'NONE', #75278, 999.9999999999998863 ) ;
#118592=VERTEX_POINT ( 'NONE', #116388 ) ;
#118593=EDGE_CURVE ( 'NONE', #134353, #108000, #39566, .T. ) ;
#118594=CARTESIAN_POINT ( 'NONE',  ( 68.99451991528748351, 28.92564299267986172, 4.000000000000000000 ) ) ;
#118595=ORIENTED_EDGE ( 'NONE', *, *, #115262, .F. ) ;
#118598=DIRECTION ( 'NONE',  ( -0.000000000000000000, -0.3543493200069152693, 0.9351131265310292928 ) ) ;
#118600=ORIENTED_EDGE ( 'NONE', *, *, #100107, .T. ) ;
#118601=EDGE_CURVE ( 'NONE', #118193, #131497, #60623, .T. ) ;
#118602=FACE_OUTER_BOUND ( 'NONE', #76068, .T. ) ;
#118604=CARTESIAN_POINT ( 'NONE',  ( 42.29974487139158157, -27.71228299555235708, 4.000000000000000000 ) ) ;
#118605=CARTESIAN_POINT ( 'NONE',  ( 26.99999999999980815, 1.931123077392165488, 4.000000000000000000 ) ) ;
#118606=LINE ( 'NONE', #33081, #50915 ) ;
#118607=CARTESIAN_POINT ( 'NONE',  ( -6.489213562373093325, -27.52281430457059841, 5.000000000000000000 ) ) ;
#118608=ORIENTED_EDGE ( 'NONE', *, *, #47562, .T. ) ;
#118609=DIRECTION ( 'NONE',  ( 0.3543493200069162685, -0.000000000000000000, -0.9351131265310288487 ) ) ;
#118610=AXIS2_PLACEMENT_3D ( 'NONE', #66898, #98100, #111080 ) ;
#118616=ORIENTED_EDGE ( 'NONE', *, *, #9655, .T. ) ;
#118617=CARTESIAN_POINT ( 'NONE',  ( -35.99451991528749772, 28.92564299267963079, 4.000000000000000000 ) ) ;
#118618=ADVANCED_FACE ( 'NONE', ( #128004 ), #53255, .F. ) ;
#118619=CARTESIAN_POINT ( 'NONE',  ( -7.499999999999940492, -5.947814304570770538, 5.000000000000000000 ) ) ;
#118620=LINE ( 'NONE', #119324, #78012 ) ;
#118621=ORIENTED_EDGE ( 'NONE', *, *, #62707, .T. ) ;
#118622=VECTOR ( 'NONE', #117292, 1000.000000000000000 ) ;
#118623=VECTOR ( 'NONE', #35490, 1000.000000000000000 ) ;
#118624=VECTOR ( 'NONE', #100648, 1000.000000000000000 ) ;
#118625=CARTESIAN_POINT ( 'NONE',  ( 24.18398860626899705, 28.73617430169804265, 5.000000000000000000 ) ) ;
#118627=ADVANCED_FACE ( 'NONE', ( #96048 ), #6867, .F. ) ;
#118630=AXIS2_PLACEMENT_3D ( 'NONE', #93533, #70406, #114554 ) ;
#118632=CARTESIAN_POINT ( 'NONE',  ( 17.99999999999987566, 13.55218569542903140, 5.000000000000000000 ) ) ;
#118633=AXIS2_PLACEMENT_3D ( 'NONE', #92941, #126981, #39290 ) ;
#118634=CARTESIAN_POINT ( 'NONE',  ( -14.20710678118644488, 9.759292476615623713, 5.000000000000000000 ) ) ;
#118635=PLANE ( 'NONE',  #49309 ) ;
#118636=VECTOR ( 'NONE', #890, 999.9999999999998863 ) ;
#118638=EDGE_CURVE ( 'NONE', #21943, #68002, #31529, .T. ) ;
#118639=ORIENTED_EDGE ( 'NONE', *, *, #68612, .F. ) ;
#118640=ORIENTED_EDGE ( 'NONE', *, *, #82160, .F. ) ;
#118641=EDGE_CURVE ( 'NONE', #62908, #28061, #141727, .T. ) ;
#118642=CARTESIAN_POINT ( 'NONE',  ( 66.48921356237309510, -27.52281430457101763, 5.000000000000000000 ) ) ;
#118643=EDGE_CURVE ( 'NONE', #83478, #122408, #9755, .T. ) ;
#118645=DIRECTION ( 'NONE',  ( -0.7071067811865487940, 0.7071067811865463515, -0.000000000000000000 ) ) ;
#118647=DIRECTION ( 'NONE',  ( -0.6830127018922181881, 0.6830127018922202975, -0.2588190451025214056 ) ) ;
#118648=CARTESIAN_POINT ( 'NONE',  ( 15.18398860626900237, 28.73617430169797871, 5.000000000000000000 ) ) ;
#118653=ORIENTED_EDGE ( 'NONE', *, *, #108259, .T. ) ;
#118654=ORIENTED_EDGE ( 'NONE', *, *, #79594, .F. ) ;
#118655=ADVANCED_FACE ( 'NONE', ( #95341 ), #119921, .F. ) ;
#118659=VECTOR ( 'NONE', #15238, 1000.000000000000000 ) ;
#118661=LINE ( 'NONE', #53406, #107286 ) ;
#118664=CARTESIAN_POINT ( 'NONE',  ( -8.994519915287490619, 28.92564299267944250, 4.000000000000000000 ) ) ;
#118665=VECTOR ( 'NONE', #80932, 1000.000000000000227 ) ;
#118667=CARTESIAN_POINT ( 'NONE',  ( -19.05000000000000071, 3.174999999999997158, 4.000000000000000000 ) ) ;
#118668=VECTOR ( 'NONE', #81563, 1000.000000000000000 ) ;
#118670=CARTESIAN_POINT ( 'NONE',  ( -1.171830600776462061, -14.24070752338414358, 4.000000000000000000 ) ) ;
#118672=PLANE ( 'NONE',  #14845 ) ;
#118673=CARTESIAN_POINT ( 'NONE',  ( -33.29974487139158867, -27.71228299555229313, 4.000000000000000000 ) ) ;
#118674=VERTEX_POINT ( 'NONE', #74331 ) ;
#118675=LINE ( 'NONE', #40428, #48202 ) ;
#118676=ORIENTED_EDGE ( 'NONE', *, *, #140704, .F. ) ;
#118677=ORIENTED_EDGE ( 'NONE', *, *, #125743, .F. ) ;
#118679=VERTEX_POINT ( 'NONE', #64162 ) ;
#118680=ORIENTED_EDGE ( 'NONE', *, *, #70044, .F. ) ;
#118681=EDGE_CURVE ( 'NONE', #70528, #50028, #129389, .T. ) ;
#118684=CARTESIAN_POINT ( 'NONE',  ( -20.14994871458963033, -8.240707523384193323, 17.25253755692234492 ) ) ;
#118686=DIRECTION ( 'NONE',  ( 0.6830127018922181881, 0.6830127018922202975, -0.2588190451025214056 ) ) ;
#118687=VECTOR ( 'NONE', #105959, 1000.000000000000000 ) ;
#118688=CARTESIAN_POINT ( 'NONE',  ( -33.18398860626899705, 28.73617430169810305, 5.000000000000000000 ) ) ;
#118689=VECTOR ( 'NONE', #111267, 1000.000000000000000 ) ;
#118690=EDGE_CURVE ( 'NONE', #104350, #94114, #30078, .T. ) ;
#118691=DIRECTION ( 'NONE',  ( -0.7071067811865486830, -0.7071067811865464625, 0.000000000000000000 ) ) ;
#118693=CARTESIAN_POINT ( 'NONE',  ( 32.12514619309215647, -14.24070752338413115, 9.401115078912585687 ) ) ;
#118694=VERTEX_POINT ( 'NONE', #108322 ) ;
#118696=EDGE_LOOP ( 'NONE', ( #111859, #25120, #52551, #136017 ) ) ;
#118697=VERTEX_POINT ( 'NONE', #8993 ) ;
#118698=EDGE_LOOP ( 'NONE', ( #135999, #115529, #66144, #140781 ) ) ;
#118699=VECTOR ( 'NONE', #129498, 1000.000000000000000 ) ;
#118701=DIRECTION ( 'NONE',  ( -0.3543493200069162685, -0.000000000000000000, -0.9351131265310288487 ) ) ;
#118703=CARTESIAN_POINT ( 'NONE',  ( 17.99999999999986855, -0.2811185226894163947, -5.995736974527558161 ) ) ;
#118704=VERTEX_POINT ( 'NONE', #107642 ) ;
#118706=AXIS2_PLACEMENT_3D ( 'NONE', #3409, #13569, #14307 ) ;
#118707=ORIENTED_EDGE ( 'NONE', *, *, #74400, .T. ) ;
#118709=LINE ( 'NONE', #19403, #89969 ) ;
#118710=DIRECTION ( 'NONE',  ( 0.6830127018922181881, 0.6830127018922202975, -0.2588190451025214056 ) ) ;
#118711=VERTEX_POINT ( 'NONE', #84497 ) ;
#118712=VERTEX_POINT ( 'NONE', #118519 ) ;
#118714=CARTESIAN_POINT ( 'NONE',  ( 17.99999999999987566, -7.447814304570745669, 5.000000000000000000 ) ) ;
#118715=CARTESIAN_POINT ( 'NONE',  ( -54.29974487139159578, -27.71228299555243879, 4.000000000000000000 ) ) ;
#118717=CARTESIAN_POINT ( 'NONE',  ( 16.82816939922341959, 21.75929247661549581, 4.000000000000000000 ) ) ;
#118718=DIRECTION ( 'NONE',  ( -0.000000000000000000, -1.000000000000000000, -0.000000000000000000 ) ) ;
#118719=AXIS2_PLACEMENT_3D ( 'NONE', #129220, #63989, #140805 ) ;
#118720=PLANE ( 'NONE',  #6270 ) ;
#118721=VECTOR ( 'NONE', #47068, 999.9999999999998863 ) ;
#118722=EDGE_CURVE ( 'NONE', #114222, #106767, #18465, .T. ) ;
#118723=DIRECTION ( 'NONE',  ( 1.000000000000000000, 0.000000000000000000, 0.000000000000000000 ) ) ;
#118725=PLANE ( 'NONE',  #30152 ) ;
#118727=ORIENTED_EDGE ( 'NONE', *, *, #38165, .F. ) ;
#118728=CARTESIAN_POINT ( 'NONE',  ( -20.99999999999985789, 20.70535890316559957, 1.956823837851964676 ) ) ;
#118729=VECTOR ( 'NONE', #11871, 1000.000000000000000 ) ;
#118730=AXIS2_PLACEMENT_3D ( 'NONE', #104125, #117159, #4791 ) ;
#118733=ADVANCED_FACE ( 'NONE', ( #119228 ), #62745, .F. ) ;
#118734=CARTESIAN_POINT ( 'NONE',  ( 42.48921356237308800, -27.52281430457085065, 5.000000000000000000 ) ) ;
#118736=ORIENTED_EDGE ( 'NONE', *, *, #35021, .T. ) ;
#118737=EDGE_CURVE ( 'NONE', #112685, #37409, #52552, .T. ) ;
#118738=DIRECTION ( 'NONE',  ( -0.000000000000000000, 0.3543493200069153248, 0.9351131265310292928 ) ) ;
#118739=VERTEX_POINT ( 'NONE', #85896 ) ;
#118740=DIRECTION ( 'NONE',  ( 0.3543493200069162685, -0.000000000000000000, -0.9351131265310288487 ) ) ;
#118741=VERTEX_POINT ( 'NONE', #130136 ) ;
#118742=EDGE_CURVE ( 'NONE', #71945, #17161, #286, .T. ) ;
#118743=EDGE_CURVE ( 'NONE', #100040, #37058, #23494, .T. ) ;
#118744=CARTESIAN_POINT ( 'NONE',  ( 31.49999999999979039, 10.46639925780216096, 5.000000000000000000 ) ) ;
#118746=DIRECTION ( 'NONE',  ( -0.000000000000000000, 0.3543493200069153248, 0.9351131265310292928 ) ) ;
#118747=VECTOR ( 'NONE', #81513, 1000.000000000000000 ) ;
#118749=ADVANCED_FACE ( 'NONE', ( #33688 ), #1010, .T. ) ;
#118750=DIRECTION ( 'NONE',  ( -0.3543493200069162685, -0.000000000000000000, -0.9351131265310288487 ) ) ;
#118751=DIRECTION ( 'NONE',  ( 0.3543493200069162685, -0.000000000000000000, -0.9351131265310288487 ) ) ;
#118752=FACE_OUTER_BOUND ( 'NONE', #62108, .T. ) ;
#118756=CARTESIAN_POINT ( 'NONE',  ( 54.48921356237310221, -27.52281430457093236, 5.000000000000000000 ) ) ;
#118757=ORIENTED_EDGE ( 'NONE', *, *, #113676, .F. ) ;
#118758=VECTOR ( 'NONE', #31861, 1000.000000000000227 ) ;
#118759=ORIENTED_EDGE ( 'NONE', *, *, #24396, .F. ) ;
#118761=CARTESIAN_POINT ( 'NONE',  ( -63.48921356237309510, -27.52281430457099631, 5.000000000000000000 ) ) ;
#118764=AXIS2_PLACEMENT_3D ( 'NONE', #35859, #13321, #25645 ) ;
#118765=LINE ( 'NONE', #86872, #89645 ) ;
#118766=DIRECTION ( 'NONE',  ( 0.7071067811865486830, -0.7071067811865464625, -0.000000000000000000 ) ) ;
#118768=ORIENTED_EDGE ( 'NONE', *, *, #15228, .T. ) ;
#118769=EDGE_CURVE ( 'NONE', #2157, #33478, #21364, .T. ) ;
#118770=CARTESIAN_POINT ( 'NONE',  ( -34.45011844616454511, 3.002304141593926001, 5.000000000000000888 ) ) ;
#118772=CARTESIAN_POINT ( 'NONE',  ( 69.29974487139159578, -27.71228299555254537, 4.000000000000000000 ) ) ;
#118773=PLANE ( 'NONE',  #40192 ) ;
#118774=FACE_OUTER_BOUND ( 'NONE', #16477, .T. ) ;
#118775=ORIENTED_EDGE ( 'NONE', *, *, #136145, .T. ) ;
#118777=EDGE_CURVE ( 'NONE', #9875, #68247, #135152, .T. ) ;
#118779=LINE ( 'NONE', #9265, #14613 ) ;
#118780=CARTESIAN_POINT ( 'NONE',  ( 51.48921356237309510, -27.52281430457091460, 5.000000000000000000 ) ) ;
#118781=( BOUNDED_CURVE ( )  B_SPLINE_CURVE ( 3, ( #10840, #68851, #134829, #44239 ),
 .UNSPECIFIED., .F., .T. ) 
 B_SPLINE_CURVE_WITH_KNOTS ( ( 4, 4 ),
 ( 1.208578181583247257, 1.359146454359469125 ),
 .UNSPECIFIED. ) 
 CURVE ( )  GEOMETRIC_REPRESENTATION_ITEM ( )  RATIONAL_B_SPLINE_CURVE ( ( 1.000000000000000000, 0.9981116584018947524, 0.9981116584018947524, 1.000000000000000000 ) ) 
 REPRESENTATION_ITEM ( '' )  );
#118783=ORIENTED_EDGE ( 'NONE', *, *, #25136, .T. ) ;
#118784=ORIENTED_EDGE ( 'NONE', *, *, #95723, .T. ) ;
#118787=VECTOR ( 'NONE', #102534, 1000.000000000000000 ) ;
#118790=EDGE_CURVE ( 'NONE', #4524, #69699, #133010, .T. ) ;
#118791=DIRECTION ( 'NONE',  ( 0.6830127018922181881, 0.6830127018922202975, -0.2588190451025214056 ) ) ;
#118792=AXIS2_PLACEMENT_3D ( 'NONE', #14481, #23942, #90632 ) ;
#118793=CARTESIAN_POINT ( 'NONE',  ( 35.99451991528749772, 28.92564299267963079, 4.000000000000000000 ) ) ;
#118794=ORIENTED_EDGE ( 'NONE', *, *, #47082, .F. ) ;
#118795=LINE ( 'NONE', #29632, #2784 ) ;
#118796=CARTESIAN_POINT ( 'NONE',  ( 33.29974487139158867, -27.71228299555229313, 4.000000000000000000 ) ) ;
#118797=EDGE_CURVE ( 'NONE', #92018, #10755, #2995, .T. ) ;
#118799=VERTEX_POINT ( 'NONE', #110482 ) ;
#118800=EDGE_CURVE ( 'NONE', #43949, #103933, #57584, .T. ) ;
#118801=DIRECTION ( 'NONE',  ( -0.7071067811865486830, -0.7071067811865464625, -0.000000000000000000 ) ) ;
#118802=LINE ( 'NONE', #73191, #98555 ) ;
#118803=AXIS2_PLACEMENT_3D ( 'NONE', #59144, #48218, #103294 ) ;
#118805=CARTESIAN_POINT ( 'NONE',  ( 10.49999999999992895, -2.568876922607790103, 4.000000000000000000 ) ) ;
#118806=EDGE_CURVE ( 'NONE', #131683, #129739, #56886, .T. ) ;
#118807=ORIENTED_EDGE ( 'NONE', *, *, #54736, .F. ) ;
#118808=ORIENTED_EDGE ( 'NONE', *, *, #143521, .T. ) ;
#118809=ORIENTED_EDGE ( 'NONE', *, *, #34511, .F. ) ;
#118810=CARTESIAN_POINT ( 'NONE',  ( 8.999999999999934275, -10.06887692260770706, 4.000000000000000000 ) ) ;
#118811=PLANE ( 'NONE',  #17620 ) ;
#118813=VECTOR ( 'NONE', #83718, 1000.000000000000227 ) ;
#118814=DIRECTION ( 'NONE',  ( -0.7071067811865486830, -0.7071067811865464625, 0.000000000000000000 ) ) ;
#118815=CARTESIAN_POINT ( 'NONE',  ( 34.45011844616451668, 12.00230414159381453, 5.000000000000000888 ) ) ;
#118817=ORIENTED_EDGE ( 'NONE', *, *, #85028, .F. ) ;
#118818=ORIENTED_EDGE ( 'NONE', *, *, #38711, .F. ) ;
#118819=EDGE_CURVE ( 'NONE', #101003, #114903, #116893, .T. ) ;
#118820=LINE ( 'NONE', #139181, #82782 ) ;
#118822=VERTEX_POINT ( 'NONE', #55427 ) ;
#118823=VECTOR ( 'NONE', #96239, 1000.000000000000227 ) ;
#118824=EDGE_CURVE ( 'NONE', #16046, #29609, #99611, .T. ) ;
#118826=DIRECTION ( 'NONE',  ( 0.7071067811865486830, -0.7071067811865464625, -0.000000000000000000 ) ) ;
#118827=DIRECTION ( 'NONE',  ( -0.7071067811865486830, -0.7071067811865464625, -0.000000000000000000 ) ) ;
#118828=VERTEX_POINT ( 'NONE', #88780 ) ;
#118829=DIRECTION ( 'NONE',  ( -1.000000000000000000, 0.000000000000000000, 0.000000000000000000 ) ) ;
#118831=LINE ( 'NONE', #129700, #121916 ) ;
#118834=DIRECTION ( 'NONE',  ( 0.7071067811865487940, 0.7071067811865463515, 0.000000000000000000 ) ) ;
#118835=LINE ( 'NONE', #61636, #16506 ) ;
#118836=ORIENTED_EDGE ( 'NONE', *, *, #34008, .F. ) ;
#118838=CARTESIAN_POINT ( 'NONE',  ( -0.4892135623730947680, -27.52281430457055578, 5.000000000000000000 ) ) ;
#118839=ORIENTED_EDGE ( 'NONE', *, *, #119618, .T. ) ;
#118842=EDGE_LOOP ( 'NONE', ( #21347, #141155, #45558, #70531 ) ) ;
#118844=ORIENTED_EDGE ( 'NONE', *, *, #3330, .F. ) ;
#118845=CARTESIAN_POINT ( 'NONE',  ( 28.49999999999980815, 4.087461875839198733, 4.000000000000000000 ) ) ;
#118846=EDGE_LOOP ( 'NONE', ( #112456, #58977, #98757, #51912 ) ) ;
#118847=VERTEX_POINT ( 'NONE', #1700 ) ;
#118848=VECTOR ( 'NONE', #106334, 1000.000000000000000 ) ;
#118849=VERTEX_POINT ( 'NONE', #45993 ) ;
#118853=CARTESIAN_POINT ( 'NONE',  ( 6.489213562373093325, -27.52281430457059841, 5.000000000000000000 ) ) ;
#118854=CARTESIAN_POINT ( 'NONE',  ( 11.99999999999992006, 1.761378380278694866, -6.096875308897227619 ) ) ;
#118856=LINE ( 'NONE', #19544, #42799 ) ;
#118857=CARTESIAN_POINT ( 'NONE',  ( -20.99999999999985079, -12.41253812416062807, 4.000000000000000000 ) ) ;
#118858=LINE ( 'NONE', #86250, #92086 ) ;
#118859=AXIS2_PLACEMENT_3D ( 'NONE', #55423, #122078, #109789 ) ;
#118860=DIRECTION ( 'NONE',  ( -0.7071067811865486830, -0.7071067811865464625, 0.000000000000000000 ) ) ;
#118861=CARTESIAN_POINT ( 'NONE',  ( 21.79333936457832266, 21.75929247661549226, 4.998822639870715179 ) ) ;
#118863=VECTOR ( 'NONE', #67013, 1000.000000000000227 ) ;
#118866=EDGE_LOOP ( 'NONE', ( #108006, #89186, #30179, #77337 ) ) ;
#118868=VERTEX_POINT ( 'NONE', #90923 ) ;
#118869=CARTESIAN_POINT ( 'NONE',  ( 19.58990935480156992, 9.759292476615625489, 11.28811694763783180 ) ) ;
#118870=VERTEX_POINT ( 'NONE', #22744 ) ;
#118871=AXIS2_PLACEMENT_3D ( 'NONE', #66324, #9010, #97486 ) ;
#118875=CARTESIAN_POINT ( 'NONE',  ( -18.00548008471250583, 28.92564299267925776, 4.000000000000000000 ) ) ;
#118876=ORIENTED_EDGE ( 'NONE', *, *, #8084, .F. ) ;
#118877=PLANE ( 'NONE',  #48778 ) ;
#118878=VERTEX_POINT ( 'NONE', #44586 ) ;
#118879=DIRECTION ( 'NONE',  ( 0.000000000000000000, 0.000000000000000000, -1.000000000000000000 ) ) ;
#118880=VECTOR ( 'NONE', #65761, 1000.000000000000000 ) ;
#118881=LINE ( 'NONE', #52199, #98310 ) ;
#118882=AXIS2_PLACEMENT_3D ( 'NONE', #123896, #69516, #2796 ) ;
#118884=VERTEX_POINT ( 'NONE', #67012 ) ;
#118886=LINE ( 'NONE', #3163, #87612 ) ;
#118887=DIRECTION ( 'NONE',  ( -0.7071067811865487940, 0.7071067811865463515, 0.000000000000000000 ) ) ;
#118888=FACE_OUTER_BOUND ( 'NONE', #30922, .T. ) ;
#118889=ORIENTED_EDGE ( 'NONE', *, *, #57135, .T. ) ;
#118890=ORIENTED_EDGE ( 'NONE', *, *, #51693, .F. ) ;
#118891=DIRECTION ( 'NONE',  ( -0.7071067811865487940, 0.7071067811865463515, -0.000000000000000000 ) ) ;
#118894=CARTESIAN_POINT ( 'NONE',  ( 54.29974487139159578, -27.71228299555243879, 4.000000000000000000 ) ) ;
#118895=CARTESIAN_POINT ( 'NONE',  ( -34.45011844616454511, -13.48371918836238059, 5.000000000000000888 ) ) ;
#118896=CARTESIAN_POINT ( 'NONE',  ( 7.001930566820925961, -22.22500000000000142, 4.500000000000000888 ) ) ;
#118897=EDGE_LOOP ( 'NONE', ( #48104, #99310, #28770, #130041 ) ) ;
#118899=LINE ( 'NONE', #51532, #111683 ) ;
#118900=VERTEX_POINT ( 'NONE', #2429 ) ;
#118901=LINE ( 'NONE', #19593, #76731 ) ;
#118902=AXIS2_PLACEMENT_3D ( 'NONE', #101051, #135842, #134429 ) ;
#118903=DIRECTION ( 'NONE',  ( -0.7071067811865486830, -0.7071067811865464625, 0.000000000000000000 ) ) ;
#118904=ORIENTED_EDGE ( 'NONE', *, *, #108301, .T. ) ;
#118906=ORIENTED_EDGE ( 'NONE', *, *, #42304, .F. ) ;
#118907=VERTEX_POINT ( 'NONE', #54721 ) ;
#118908=ADVANCED_FACE ( 'NONE', ( #80063 ), #98901, .F. ) ;
#118909=EDGE_CURVE ( 'NONE', #75489, #78485, #32988, .T. ) ;
#118911=CARTESIAN_POINT ( 'NONE',  ( 16.49999999999988631, 21.43112307739196609, 4.000000000000000000 ) ) ;
#118912=DIRECTION ( 'NONE',  ( -0.7071067811865487940, 0.7071067811865463515, 0.000000000000000000 ) ) ;
#118913=EDGE_LOOP ( 'NONE', ( #26461, #119684, #26667, #103881 ) ) ;
#118914=LINE ( 'NONE', #87008, #116042 ) ;
#118915=EDGE_CURVE ( 'NONE', #130332, #124489, #82896, .T. ) ;
#118917=CARTESIAN_POINT ( 'NONE',  ( -32.75830541574792676, 0.7592924766157104211, 14.37146558664990259 ) ) ;
#118918=DIRECTION ( 'NONE',  ( -0.6830127018922180770, -0.6830127018922204085, -0.2588190451025213501 ) ) ;
#118919=AXIS2_PLACEMENT_3D ( 'NONE', #13462, #125106, #90338 ) ;
#118922=EDGE_CURVE ( 'NONE', #93631, #68320, #94454, .T. ) ;
#118923=DIRECTION ( 'NONE',  ( -0.7071067811865486830, -0.7071067811865464625, 0.000000000000000000 ) ) ;
#118924=LINE ( 'NONE', #50122, #88769 ) ;
#118925=FACE_OUTER_BOUND ( 'NONE', #52607, .T. ) ;
#118926=PLANE ( 'NONE',  #62972 ) ;
#118927=CARTESIAN_POINT ( 'NONE',  ( -11.67183060077638501, 2.259292476615694323, 4.000000000000000000 ) ) ;
#118928=EDGE_CURVE ( 'NONE', #14639, #93058, #24917, .T. ) ;
#118929=CARTESIAN_POINT ( 'NONE',  ( -15.48921356237309510, -27.52281430457066236, 5.000000000000000000 ) ) ;
#118930=DIRECTION ( 'NONE',  ( -0.7071067811865486830, 0.7071067811865464625, 0.000000000000000000 ) ) ;
#118931=VERTEX_POINT ( 'NONE', #81484 ) ;
#118932=AXIS2_PLACEMENT_3D ( 'NONE', #32594, #100701, #76828 ) ;
#118933=ORIENTED_EDGE ( 'NONE', *, *, #139906, .T. ) ;
#118934=ORIENTED_EDGE ( 'NONE', *, *, #139529, .T. ) ;
#118936=EDGE_CURVE ( 'NONE', #79481, #78193, #103192, .T. ) ;
#118937=EDGE_LOOP ( 'NONE', ( #58785, #102390, #39213, #120922 ) ) ;
#118939=ORIENTED_EDGE ( 'NONE', *, *, #44710, .T. ) ;
#118940=LINE ( 'NONE', #10175, #142845 ) ;
#118942=ORIENTED_EDGE ( 'NONE', *, *, #109201, .F. ) ;
#118943=LINE ( 'NONE', #22464, #87952 ) ;
#118944=EDGE_CURVE ( 'NONE', #50064, #88923, #103885, .T. ) ;
#118945=DIRECTION ( 'NONE',  ( -0.7071067811865487940, 0.7071067811865463515, 0.000000000000000000 ) ) ;
#118946=CARTESIAN_POINT ( 'NONE',  ( 13.10966639810773948, 3.759292476615678336, 4.164048746910661514 ) ) ;
#118947=CARTESIAN_POINT ( 'NONE',  ( 36.18398860626899705, 28.73617430169812437, 5.000000000000000000 ) ) ;
#118949=VERTEX_POINT ( 'NONE', #48122 ) ;
#118951=CARTESIAN_POINT ( 'NONE',  ( -15.79076468313838433, 8.175634574663693144, 5.000000000000000000 ) ) ;
#118954=DIRECTION ( 'NONE',  ( 0.3543493200069162685, -0.000000000000000000, -0.9351131265310288487 ) ) ;
#118955=LINE ( 'NONE', #10878, #124069 ) ;
#118956=FACE_OUTER_BOUND ( 'NONE', #86985, .T. ) ;
#118957=CARTESIAN_POINT ( 'NONE',  ( -27.70710678118634362, -15.74070752338411694, 5.000000000000000000 ) ) ;
#118958=VECTOR ( 'NONE', #15142, 999.9999999999998863 ) ;
#118959=ORIENTED_EDGE ( 'NONE', *, *, #55023, .F. ) ;
#118960=ORIENTED_EDGE ( 'NONE', *, *, #56005, .F. ) ;
#118962=ORIENTED_EDGE ( 'NONE', *, *, #15723, .F. ) ;
#118963=DIRECTION ( 'NONE',  ( 0.000000000000000000, -1.000000000000000000, 0.000000000000000000 ) ) ;
#118964=EDGE_CURVE ( 'NONE', #48040, #59390, #92304, .T. ) ;
#118966=LINE ( 'NONE', #97178, #20232 ) ;
#118967=VECTOR ( 'NONE', #63983, 999.9999999999998863 ) ;
#118968=LINE ( 'NONE', #19661, #111492 ) ;
#118971=EDGE_CURVE ( 'NONE', #115630, #46893, #5987, .T. ) ;
#118973=VECTOR ( 'NONE', #100193, 1000.000000000000000 ) ;
#118974=ORIENTED_EDGE ( 'NONE', *, *, #16835, .F. ) ;
#118977=CARTESIAN_POINT ( 'NONE',  ( 2.510786437626908008, -27.52281430457053446, 5.000000000000000000 ) ) ;
#118978=ORIENTED_EDGE ( 'NONE', *, *, #72676, .F. ) ;
#118981=ADVANCED_FACE ( 'NONE', ( #80759 ), #50265, .T. ) ;
#118982=AXIS2_PLACEMENT_3D ( 'NONE', #48854, #106036, #139455 ) ;
#118983=EDGE_CURVE ( 'NONE', #109290, #19069, #26365, .T. ) ;
#118984=DIRECTION ( 'NONE',  ( 0.7071067811865486830, -0.7071067811865464625, -0.000000000000000000 ) ) ;
#118987=AXIS2_PLACEMENT_3D ( 'NONE', #119748, #19039, #124073 ) ;
#118988=ORIENTED_EDGE ( 'NONE', *, *, #94261, .F. ) ;
#118989=LINE ( 'NONE', #76209, #61055 ) ;
#118990=DIRECTION ( 'NONE',  ( 0.7071067811865486830, -0.7071067811865464625, -0.000000000000000000 ) ) ;
#118991=CARTESIAN_POINT ( 'NONE',  ( -3.183988606268992161, 28.73617430169789699, 5.000000000000000000 ) ) ;
#118996=EDGE_CURVE ( 'NONE', #44540, #52184, #113343, .T. ) ;
#118997=LINE ( 'NONE', #42178, #101172 ) ;
#118999=VERTEX_POINT ( 'NONE', #49573 ) ;
#119000=VECTOR ( 'NONE', #97533, 1000.000000000000227 ) ;
#119002=DIRECTION ( 'NONE',  ( -0.7071067811865486830, -0.7071067811865464625, 0.000000000000000000 ) ) ;
#119003=CARTESIAN_POINT ( 'NONE',  ( -23.29289321881329755, 17.25929247661554200, 5.000000000000000000 ) ) ;
#119004=ADVANCED_FACE ( 'NONE', ( #61183 ), #59725, .T. ) ;
#119006=LINE ( 'NONE', #19689, #140883 ) ;
#119008=DIRECTION ( 'NONE',  ( 0.7071067811865486830, -0.7071067811865464625, -0.000000000000000000 ) ) ;
#119009=PLANE ( 'NONE',  #18786 ) ;
#119010=EDGE_CURVE ( 'NONE', #107846, #27577, #114761, .T. ) ;
#119011=FACE_BOUND ( 'NONE', #39626, .T. ) ;
#119013=CARTESIAN_POINT ( 'NONE',  ( -10.82816939922345156, -5.240707523384225297, 4.000000000000000000 ) ) ;
#119014=CARTESIAN_POINT ( 'NONE',  ( -25.49999999999982236, -2.173586137069152713, -4.605770156576171281 ) ) ;
#119015=VERTEX_POINT ( 'NONE', #25629 ) ;
#119017=ORIENTED_EDGE ( 'NONE', *, *, #79102, .F. ) ;
#119019=DIRECTION ( 'NONE',  ( 0.6830127018922181881, 0.6830127018922202975, -0.2588190451025214056 ) ) ;
#119020=VERTEX_POINT ( 'NONE', #38667 ) ;
#119022=VECTOR ( 'NONE', #122435, 1000.000000000000000 ) ;
#119023=ORIENTED_EDGE ( 'NONE', *, *, #40458, .T. ) ;
#119024=LINE ( 'NONE', #132068, #51115 ) ;
#119025=LINE ( 'NONE', #29168, #26432 ) ;
#119026=VERTEX_POINT ( 'NONE', #82202 ) ;
#119027=CARTESIAN_POINT ( 'NONE',  ( 6.707106781186505273, 20.25929247661551713, 5.000000000000000000 ) ) ;
#119028=LINE ( 'NONE', #19713, #73591 ) ;
#119029=VECTOR ( 'NONE', #37931, 1000.000000000000000 ) ;
#119030=EDGE_CURVE ( 'NONE', #56450, #92514, #69906, .T. ) ;
#119031=ADVANCED_FACE ( 'NONE', ( #139442 ), #108875, .F. ) ;
#119032=CARTESIAN_POINT ( 'NONE',  ( 65.99451991528749772, 28.92564299267984396, 4.000000000000000000 ) ) ;
#119033=CARTESIAN_POINT ( 'NONE',  ( -34.92500000000001137, -5.337538124160958297, 4.000000000000000000 ) ) ;
#119034=CARTESIAN_POINT ( 'NONE',  ( -30.29974487139158867, -27.71228299555227537, 4.000000000000000000 ) ) ;
#119036=CARTESIAN_POINT ( 'NONE',  ( -12.32816939922343913, -18.74070752338409207, 4.000000000000000000 ) ) ;
#119037=VERTEX_POINT ( 'NONE', #74149 ) ;
#119038=ORIENTED_EDGE ( 'NONE', *, *, #64001, .T. ) ;
#119039=CARTESIAN_POINT ( 'NONE',  ( 32.99999999999976552, -22.22500000000000142, 4.412002311790011788 ) ) ;
#119040=FACE_OUTER_BOUND ( 'NONE', #103368, .T. ) ;
#119041=EDGE_LOOP ( 'NONE', ( #132434, #53257, #55702, #91269 ) ) ;
#119042=EDGE_LOOP ( 'NONE', ( #69902, #92085, #121566, #85831 ) ) ;
#119044=LINE ( 'NONE', #108142, #5005 ) ;
#119045=CARTESIAN_POINT ( 'NONE',  ( -57.48921356237308800, -27.52281430457095368, 5.000000000000000000 ) ) ;
#119047=CARTESIAN_POINT ( 'NONE',  ( 19.05000000000000071, 3.174999999999997158, 4.000000000000000000 ) ) ;
#119048=ORIENTED_EDGE ( 'NONE', *, *, #82878, .F. ) ;
#119049=DIRECTION ( 'NONE',  ( -0.7071067811865486830, -0.7071067811865464625, 0.000000000000000000 ) ) ;
#119050=VECTOR ( 'NONE', #92444, 1000.000000000000000 ) ;
#119051=PLANE ( 'NONE',  #2930 ) ;
#119052=AXIS2_PLACEMENT_3D ( 'NONE', #102734, #81718, #47673 ) ;
#119054=ORIENTED_EDGE ( 'NONE', *, *, #6273, .T. ) ;
#119057=LINE ( 'NONE', #53834, #136854 ) ;
#119058=LINE ( 'NONE', #19749, #95904 ) ;
#119059=CARTESIAN_POINT ( 'NONE',  ( -12.00548008471251293, 28.92564299267929684, 4.000000000000000000 ) ) ;
#119060=VERTEX_POINT ( 'NONE', #63309 ) ;
#119061=PLANE ( 'NONE',  #143475 ) ;
#119062=ORIENTED_EDGE ( 'NONE', *, *, #2026, .T. ) ;
#119064=CARTESIAN_POINT ( 'NONE',  ( -21.31657961132776435, -6.740707523384205757, 11.88629033278129477 ) ) ;
#119065=CARTESIAN_POINT ( 'NONE',  ( 0.000000000000000000, 0.000000000000000000, 5.000000000000000000 ) ) ;
#119066=ORIENTED_EDGE ( 'NONE', *, *, #5053, .T. ) ;
#119067=AXIS2_PLACEMENT_3D ( 'NONE', #35506, #71669, #136196 ) ;
#119068=FACE_OUTER_BOUND ( 'NONE', #34963, .T. ) ;
#119069=CARTESIAN_POINT ( 'NONE',  ( -4.499999999999965361, -16.91253812416058722, 4.000000000000000000 ) ) ;
#119070=VERTEX_POINT ( 'NONE', #97279 ) ;
#119071=FACE_OUTER_BOUND ( 'NONE', #126418, .T. ) ;
#119072=LINE ( 'NONE', #106034, #120994 ) ;
#119074=LINE ( 'NONE', #53857, #31039 ) ;
#119075=DIRECTION ( 'NONE',  ( -0.000000000000000000, 0.3543493200069153248, 0.9351131265310292928 ) ) ;
#119076=VECTOR ( 'NONE', #25096, 1000.000000000000000 ) ;
#119077=ORIENTED_EDGE ( 'NONE', *, *, #119931, .T. ) ;
#119079=EDGE_LOOP ( 'NONE', ( #135115, #107574, #76904, #54528 ) ) ;
#119080=CARTESIAN_POINT ( 'NONE',  ( -26.99999999999980105, 17.96639925780208102, 5.000000000000000000 ) ) ;
#119082=AXIS2_PLACEMENT_3D ( 'NONE', #113892, #14580, #39196 ) ;
#119085=EDGE_CURVE ( 'NONE', #136430, #61441, #30660, .T. ) ;
#119086=EDGE_CURVE ( 'NONE', #80231, #143132, #40125, .T. ) ;
#119087=VECTOR ( 'NONE', #98215, 1000.000000000000000 ) ;
#119089=CARTESIAN_POINT ( 'NONE',  ( -34.92500000000001137, 22.22500000000000142, 4.000000000000000000 ) ) ;
#119090=CARTESIAN_POINT ( 'NONE',  ( 29.99451991528749417, 28.92564299267958816, 4.000000000000000000 ) ) ;
#119092=ORIENTED_EDGE ( 'NONE', *, *, #76575, .T. ) ;
#119094=ADVANCED_FACE ( 'NONE', ( #142279 ), #8142, .F. ) ;
#119095=CARTESIAN_POINT ( 'NONE',  ( 31.49999999999977973, 12.43112307739205669, 4.000000000000000000 ) ) ;
#119096=LINE ( 'NONE', #72804, #102632 ) ;
#119098=EDGE_CURVE ( 'NONE', #112107, #111218, #7432, .T. ) ;
#119100=AXIS2_PLACEMENT_3D ( 'NONE', #106162, #139577, #107613 ) ;
#119101=ORIENTED_EDGE ( 'NONE', *, *, #29370, .T. ) ;
#119102=DIRECTION ( 'NONE',  ( 0.3543493200069163240, 0.000000000000000000, -0.9351131265310288487 ) ) ;
#119103=ADVANCED_FACE ( 'NONE', ( #141550 ), #50972, .T. ) ;
#119104=VERTEX_POINT ( 'NONE', #61865 ) ;
#119105=EDGE_CURVE ( 'NONE', #65901, #104855, #84340, .T. ) ;
#119106=ORIENTED_EDGE ( 'NONE', *, *, #106433, .T. ) ;
#119107=DIRECTION ( 'NONE',  ( 0.000000000000000000, -1.000000000000000000, 0.000000000000000000 ) ) ;
#119108=DIRECTION ( 'NONE',  ( 0.7071067811865487940, 0.7071067811865463515, -0.000000000000000000 ) ) ;
#119109=EDGE_LOOP ( 'NONE', ( #61005, #61134, #134944, #5484, #122267 ) ) ;
#119111=DIRECTION ( 'NONE',  ( -0.7071067811865486830, -0.7071067811865464625, 0.000000000000000000 ) ) ;
#119113=DIRECTION ( 'NONE',  ( -0.7071067811865487940, 0.7071067811865463515, 0.000000000000000000 ) ) ;
#119114=ADVANCED_FACE ( 'NONE', ( #6695 ), #85714, .T. ) ;
#119115=PLANE ( 'NONE',  #39582 ) ;
#119118=CARTESIAN_POINT ( 'NONE',  ( 3.183988606268992161, 28.73617430169789699, 5.000000000000000000 ) ) ;
#119119=LINE ( 'NONE', #116976, #37633 ) ;
#119122=CARTESIAN_POINT ( 'NONE',  ( 10.82816939922345156, -17.24070752338410628, 4.000000000000000000 ) ) ;
#119123=ADVANCED_FACE ( 'NONE', ( #128536 ), #73444, .T. ) ;
#119124=CARTESIAN_POINT ( 'NONE',  ( 18.48921356237309510, -27.52281430457068367, 5.000000000000000000 ) ) ;
#119126=FACE_OUTER_BOUND ( 'NONE', #110739, .T. ) ;
#119127=ORIENTED_EDGE ( 'NONE', *, *, #20349, .T. ) ;
#119128=ORIENTED_EDGE ( 'NONE', *, *, #74603, .T. ) ;
#119130=CARTESIAN_POINT ( 'NONE',  ( -14.70025512860841133, -27.71228299555195917, 4.000000000000000000 ) ) ;
#119131=CARTESIAN_POINT ( 'NONE',  ( -36.31657961132766843, -6.740707523384205757, 11.88629033278132852 ) ) ;
#119132=ORIENTED_EDGE ( 'NONE', *, *, #96612, .T. ) ;
#119136=ORIENTED_EDGE ( 'NONE', *, *, #57741, .T. ) ;
#119137=EDGE_CURVE ( 'NONE', #139318, #18266, #108160, .T. ) ;
#119139=ORIENTED_EDGE ( 'NONE', *, *, #1643, .T. ) ;
#119140=ORIENTED_EDGE ( 'NONE', *, *, #20367, .F. ) ;
#119144=CARTESIAN_POINT ( 'NONE',  ( -23.99999999999982592, 7.552185695429090906, 5.000000000000000000 ) ) ;
#119146=FACE_OUTER_BOUND ( 'NONE', #96637, .T. ) ;
#119147=CARTESIAN_POINT ( 'NONE',  ( 4.499999999999972466, 16.46639925780209524, 5.000000000000000000 ) ) ;
#119148=EDGE_LOOP ( 'NONE', ( #84829, #134144, #75915, #50841 ) ) ;
#119150=DIRECTION ( 'NONE',  ( 0.3543493200069162685, -0.000000000000000000, -0.9351131265310288487 ) ) ;
#119151=DIRECTION ( 'NONE',  ( -0.6830127018922181881, 0.6830127018922202975, -0.2588190451025214056 ) ) ;
#119152=VECTOR ( 'NONE', #66285, 1000.000000000000000 ) ;
#119153=DIRECTION ( 'NONE',  ( -0.000000000000000000, 0.3543493200069153248, 0.9351131265310292928 ) ) ;
#119155=AXIS2_PLACEMENT_3D ( 'NONE', #24637, #136977, #105051 ) ;
#119156=ORIENTED_EDGE ( 'NONE', *, *, #117790, .T. ) ;
#119157=( BOUNDED_CURVE ( )  B_SPLINE_CURVE ( 3, ( #80331, #4096, #114352, #124519 ),
 .UNSPECIFIED., .F., .T. ) 
 B_SPLINE_CURVE_WITH_KNOTS ( ( 4, 4 ),
 ( 4.517163242187656635, 4.562733109340372906 ),
 .UNSPECIFIED. ) 
 CURVE ( )  GEOMETRIC_REPRESENTATION_ITEM ( )  RATIONAL_B_SPLINE_CURVE ( ( 1.000000000000000000, 0.9998269564205118920, 0.9998269564205118920, 1.000000000000000000 ) ) 
 REPRESENTATION_ITEM ( '' )  );
#119160=AXIS2_PLACEMENT_3D ( 'NONE', #93100, #93807, #25690 ) ;
#119161=FACE_OUTER_BOUND ( 'NONE', #138517, .T. ) ;
#119163=CARTESIAN_POINT ( 'NONE',  ( -41.99451991528749062, 28.92564299267967343, 4.000000000000000000 ) ) ;
#119164=CARTESIAN_POINT ( 'NONE',  ( -27.70710678118635073, 20.25929247661551003, 5.000000000000000000 ) ) ;
#119165=EDGE_LOOP ( 'NONE', ( #102130, #47072, #56888, #53734 ) ) ;
#119166=ORIENTED_EDGE ( 'NONE', *, *, #66692, .F. ) ;
#119167=LINE ( 'NONE', #12546, #104820 ) ;
#119168=ORIENTED_EDGE ( 'NONE', *, *, #32369, .T. ) ;
#119169=VERTEX_POINT ( 'NONE', #41503 ) ;
#119171=ADVANCED_FACE ( 'NONE', ( #34217 ), #101592, .F. ) ;
#119173=ORIENTED_EDGE ( 'NONE', *, *, #125210, .F. ) ;
#119174=PLANE ( 'NONE',  #93172 ) ;
#119175=DIRECTION ( 'NONE',  ( -0.7071067811865486830, -0.7071067811865464625, 0.000000000000000000 ) ) ;
#119176=CARTESIAN_POINT ( 'NONE',  ( -34.49999999999976552, -14.94567065516890558, 4.994342998332162331 ) ) ;
#119177=ADVANCED_FACE ( 'NONE', ( #111776 ), #110311, .F. ) ;
#119178=FACE_BOUND ( 'NONE', #42837, .T. ) ;
#119179=PLANE ( 'NONE',  #128874 ) ;
#119180=DIRECTION ( 'NONE',  ( 0.7071067811865487940, 0.7071067811865463515, 0.000000000000000000 ) ) ;
#119181=DIRECTION ( 'NONE',  ( -0.6830127018922180770, -0.6830127018922204085, -0.2588190451025213501 ) ) ;
#119182=CARTESIAN_POINT ( 'NONE',  ( 32.99999999999977973, 5.587461875839189851, 4.000000000000000000 ) ) ;
#119183=ORIENTED_EDGE ( 'NONE', *, *, #81942, .T. ) ;
#119184=CARTESIAN_POINT ( 'NONE',  ( -27.29974487139158512, -27.71228299555225405, 4.000000000000000000 ) ) ;
#119185=VECTOR ( 'NONE', #120727, 1000.000000000000000 ) ;
#119188=VECTOR ( 'NONE', #6307, 1000.000000000000000 ) ;
#119189=VERTEX_POINT ( 'NONE', #100192 ) ;
#119191=VERTEX_POINT ( 'NONE', #11704 ) ;
#119193=LINE ( 'NONE', #108284, #32798 ) ;
#119194=ORIENTED_EDGE ( 'NONE', *, *, #63217, .F. ) ;
#119195=LINE ( 'NONE', #19878, #83856 ) ;
#119196=CARTESIAN_POINT ( 'NONE',  ( -15.46160355370562023, -9.740707523384180888, 17.74957260769607359 ) ) ;
#119197=DIRECTION ( 'NONE',  ( -0.7071067811865486830, -0.7071067811865464625, -0.000000000000000000 ) ) ;
#119199=DIRECTION ( 'NONE',  ( 0.7071067811865486830, -0.7071067811865464625, -0.000000000000000000 ) ) ;
#119201=DIRECTION ( 'NONE',  ( -0.000000000000000000, 0.3543493200069153248, 0.9351131265310292928 ) ) ;
#119202=CARTESIAN_POINT ( 'NONE',  ( -34.92500000000001137, 17.56110451772267211, 6.767324343803291953 ) ) ;
#119203=CARTESIAN_POINT ( 'NONE',  ( -6.813775866939250747, -22.22500000000000142, -5.652393676757531793 ) ) ;
#119204=VERTEX_POINT ( 'NONE', #10297 ) ;
#119206=VERTEX_POINT ( 'NONE', #134247 ) ;
#119208=DIRECTION ( 'NONE',  ( -0.7071067811865486830, -0.7071067811865464625, 0.000000000000000000 ) ) ;
#119209=ORIENTED_EDGE ( 'NONE', *, *, #16279, .F. ) ;
#119210=ORIENTED_EDGE ( 'NONE', *, *, #131035, .T. ) ;
#119211=EDGE_CURVE ( 'NONE', #65878, #48062, #21895, .T. ) ;
#119212=ORIENTED_EDGE ( 'NONE', *, *, #80969, .F. ) ;
#119214=ORIENTED_EDGE ( 'NONE', *, *, #100271, .T. ) ;
#119219=ORIENTED_EDGE ( 'NONE', *, *, #21804, .F. ) ;
#119220=DIRECTION ( 'NONE',  ( -0.7071067811865486830, -0.7071067811865464625, 0.000000000000000000 ) ) ;
#119221=ORIENTED_EDGE ( 'NONE', *, *, #55667, .T. ) ;
#119222=FACE_OUTER_BOUND ( 'NONE', #20083, .T. ) ;
#119223=CARTESIAN_POINT ( 'NONE',  ( 32.34328999833767426, 3.759292476615685441, 13.27625715073272872 ) ) ;
#119224=FACE_OUTER_BOUND ( 'NONE', #134063, .T. ) ;
#119225=ORIENTED_EDGE ( 'NONE', *, *, #114206, .T. ) ;
#119226=EDGE_LOOP ( 'NONE', ( #16458, #119626, #77370, #34912 ) ) ;
#119227=EDGE_CURVE ( 'NONE', #80329, #121162, #99437, .T. ) ;
#119228=FACE_OUTER_BOUND ( 'NONE', #23367, .T. ) ;
#119229=CARTESIAN_POINT ( 'NONE',  ( 0.000000000000000000, 0.000000000000000000, 5.000000000000000000 ) ) ;
#119230=ORIENTED_EDGE ( 'NONE', *, *, #135478, .F. ) ;
#119231=DIRECTION ( 'NONE',  ( -0.3543493200069162685, -0.000000000000000000, -0.9351131265310288487 ) ) ;
#119232=EDGE_LOOP ( 'NONE', ( #48114, #94235, #57357, #53588 ) ) ;
#119233=EDGE_LOOP ( 'NONE', ( #121131, #26431, #100209, #126253 ) ) ;
#119234=ORIENTED_EDGE ( 'NONE', *, *, #42840, .F. ) ;
#119235=CARTESIAN_POINT ( 'NONE',  ( -9.005480084712511157, 28.92564299267931816, 4.000000000000000000 ) ) ;
#119236=DIRECTION ( 'NONE',  ( -0.7071067811865486830, 0.7071067811865464625, 0.000000000000000000 ) ) ;
#119237=CARTESIAN_POINT ( 'NONE',  ( 14.11162361894749395, 9.759292476615607725, 17.35367589129209520 ) ) ;
#119238=DIRECTION ( 'NONE',  ( -0.7071067811865487940, 0.7071067811865463515, 0.000000000000000000 ) ) ;
#119239=DIRECTION ( 'NONE',  ( 0.7071067811865486830, -0.7071067811865464625, -0.000000000000000000 ) ) ;
#119240=CARTESIAN_POINT ( 'NONE',  ( -39.18398860626899705, 28.73617430169814568, 5.000000000000000000 ) ) ;
#119243=ORIENTED_EDGE ( 'NONE', *, *, #121312, .T. ) ;
#119244=DIRECTION ( 'NONE',  ( -0.000000000000000000, -0.3543493200069152693, 0.9351131265310292928 ) ) ;
#119245=VECTOR ( 'NONE', #72310, 1000.000000000000000 ) ;
#119246=LINE ( 'NONE', #75778, #126954 ) ;
#119247=ADVANCED_FACE ( 'NONE', ( #78436 ), #98733, .T. ) ;
#119248=VERTEX_POINT ( 'NONE', #56725 ) ;
#119249=CARTESIAN_POINT ( 'NONE',  ( -25.49999999999982592, 3.653845994658372121, -4.504631822206310865 ) ) ;
#119250=DIRECTION ( 'NONE',  ( 0.7071067811865487940, 0.7071067811865463515, 0.000000000000000000 ) ) ;
#119251=ORIENTED_EDGE ( 'NONE', *, *, #126994, .T. ) ;
#119252=ADVANCED_FACE ( 'NONE', ( #68311 ), #142962, .F. ) ;
#119253=AXIS2_PLACEMENT_3D ( 'NONE', #103095, #81369, #35737 ) ;
#119254=VERTEX_POINT ( 'NONE', #34941 ) ;
#119255=CARTESIAN_POINT ( 'NONE',  ( -11.70025512860841133, -27.71228299555198049, 4.000000000000000000 ) ) ;
#119256=ADVANCED_FACE ( 'NONE', ( #132113 ), #79182, .F. ) ;
#119258=CARTESIAN_POINT ( 'NONE',  ( -34.45011844616455221, -17.99769585840585862, 5.000000000000000888 ) ) ;
#119260=EDGE_CURVE ( 'NONE', #126683, #73943, #132839, .T. ) ;
#119264=AXIS2_PLACEMENT_3D ( 'NONE', #694, #44244, #10844 ) ;
#119265=DIRECTION ( 'NONE',  ( -0.7071067811865487940, 0.7071067811865463515, 0.000000000000000000 ) ) ;
#119266=DIRECTION ( 'NONE',  ( 0.7071067811865487940, 0.7071067811865463515, -0.000000000000000000 ) ) ;
#119267=ORIENTED_EDGE ( 'NONE', *, *, #46508, .T. ) ;
#119268=LINE ( 'NONE', #62787, #58072 ) ;
#119269=EDGE_LOOP ( 'NONE', ( #47761, #84425, #75206, #63570 ) ) ;
#119270=CARTESIAN_POINT ( 'NONE',  ( 0.000000000000000000, 0.000000000000000000, 5.000000000000000000 ) ) ;
#119271=DIRECTION ( 'NONE',  ( -0.7071067811865486830, -0.7071067811865464625, 0.000000000000000000 ) ) ;
#119272=ORIENTED_EDGE ( 'NONE', *, *, #126142, .T. ) ;
#119274=DIRECTION ( 'NONE',  ( -0.7071067811865486830, -0.7071067811865464625, 0.000000000000000000 ) ) ;
#119275=ORIENTED_EDGE ( 'NONE', *, *, #4059, .T. ) ;
#119276=ADVANCED_FACE ( 'NONE', ( #66844 ), #33527, .F. ) ;
#119278=EDGE_CURVE ( 'NONE', #115116, #59322, #32807, .T. ) ;
#119279=DIRECTION ( 'NONE',  ( 0.6830127018922180770, -0.6830127018922204085, -0.2588190451025213501 ) ) ;
#119280=CARTESIAN_POINT ( 'NONE',  ( -15.70710678118643422, 17.25929247661554200, 5.000000000000000000 ) ) ;
#119283=DIRECTION ( 'NONE',  ( 0.7071067811865486830, -0.7071067811865464625, -0.000000000000000000 ) ) ;
#119284=CARTESIAN_POINT ( 'NONE',  ( 21.18398860626899349, 28.73617430169802134, 5.000000000000000000 ) ) ;
#119285=CARTESIAN_POINT ( 'NONE',  ( -24.18398860626899705, 28.73617430169804265, 5.000000000000000000 ) ) ;
#119286=EDGE_CURVE ( 'NONE', #125583, #25180, #131387, .T. ) ;
#119287=VECTOR ( 'NONE', #94871, 1000.000000000000000 ) ;
#119289=CARTESIAN_POINT ( 'NONE',  ( 0.4892135623730947680, -27.52281430457055578, 5.000000000000000000 ) ) ;
#119291=VECTOR ( 'NONE', #22133, 999.9999999999998863 ) ;
#119292=DIRECTION ( 'NONE',  ( 0.6830127018922181881, 0.6830127018922202975, -0.2588190451025214056 ) ) ;
#119293=EDGE_LOOP ( 'NONE', ( #54042, #32322, #94723 ) ) ;
#119294=VECTOR ( 'NONE', #29565, 1000.000000000000000 ) ;
#119295=LINE ( 'NONE', #85238, #83963 ) ;
#119296=CARTESIAN_POINT ( 'NONE',  ( 24.75860074219779605, 21.72500000000000853, 5.000000000000000000 ) ) ;
#119297=EDGE_CURVE ( 'NONE', #95628, #141405, #21184, .T. ) ;
#119298=ORIENTED_EDGE ( 'NONE', *, *, #33839, .T. ) ;
#119299=DIRECTION ( 'NONE',  ( -0.6830127018922181881, 0.6830127018922202975, -0.2588190451025214056 ) ) ;
#119300=ORIENTED_EDGE ( 'NONE', *, *, #14651, .T. ) ;
#119303=EDGE_CURVE ( 'NONE', #41681, #14410, #109618, .T. ) ;
#119305=ORIENTED_EDGE ( 'NONE', *, *, #33371, .F. ) ;
#119306=CARTESIAN_POINT ( 'NONE',  ( 17.29289321881334018, -9.740707523384179112, 5.000000000000000000 ) ) ;
#119307=CARTESIAN_POINT ( 'NONE',  ( -75.48921356237309510, -27.52281430457107803, 5.000000000000000000 ) ) ;
#119308=CARTESIAN_POINT ( 'NONE',  ( 25.49999999999983658, -17.94781430457063820, 5.000000000000000000 ) ) ;
#119310=CARTESIAN_POINT ( 'NONE',  ( 11.81601139373100651, 28.73617430169779041, 5.000000000000000000 ) ) ;
#119312=CARTESIAN_POINT ( 'NONE',  ( -36.18398860626899705, 28.73617430169812437, 5.000000000000000000 ) ) ;
#119313=CARTESIAN_POINT ( 'NONE',  ( 5.483345613589513334, 22.22500000000000142, 4.500000000000000888 ) ) ;
#119315=DIRECTION ( 'NONE',  ( 0.7071067811865487940, -0.7071067811865463515, 0.000000000000000000 ) ) ;
#119316=ORIENTED_EDGE ( 'NONE', *, *, #138109, .F. ) ;
#119317=EDGE_CURVE ( 'NONE', #47321, #85516, #104444, .T. ) ;
#119320=ORIENTED_EDGE ( 'NONE', *, *, #127973, .T. ) ;
#119321=DIRECTION ( 'NONE',  ( 0.6830127018922180770, -0.6830127018922204085, -0.2588190451025213501 ) ) ;
#119323=CARTESIAN_POINT ( 'NONE',  ( -50.99451991528749062, 28.92564299267973738, 4.000000000000000000 ) ) ;
#119324=CARTESIAN_POINT ( 'NONE',  ( 6.459838389497365441, 18.75929247661552779, 8.305906642995500633 ) ) ;
#119325=ORIENTED_EDGE ( 'NONE', *, *, #27445, .T. ) ;
#119326=CARTESIAN_POINT ( 'NONE',  ( 45.18398860626900415, 28.73617430169818832, 5.000000000000000000 ) ) ;
#119328=ORIENTED_EDGE ( 'NONE', *, *, #112198, .T. ) ;
#119329=EDGE_CURVE ( 'NONE', #115416, #136288, #92137, .T. ) ;
#119330=LINE ( 'NONE', #20018, #113910 ) ;
#119332=CARTESIAN_POINT ( 'NONE',  ( -5.843876922607543989, -22.22500000000000142, 4.000000000000000000 ) ) ;
#119333=VERTEX_POINT ( 'NONE', #27597 ) ;
#119334=ORIENTED_EDGE ( 'NONE', *, *, #81379, .F. ) ;
#119335=EDGE_CURVE ( 'NONE', #73203, #51894, #46566, .T. ) ;
#119336=FACE_BOUND ( 'NONE', #20870, .T. ) ;
#119337=CARTESIAN_POINT ( 'NONE',  ( -21.18398860626899349, 28.73617430169802134, 5.000000000000000000 ) ) ;
#119340=LINE ( 'NONE', #75874, #74316 ) ;
#119341=VECTOR ( 'NONE', #68914, 999.9999999999998863 ) ;
#119342=ORIENTED_EDGE ( 'NONE', *, *, #130554, .F. ) ;
#119347=ORIENTED_EDGE ( 'NONE', *, *, #114544, .T. ) ;
#119349=CARTESIAN_POINT ( 'NONE',  ( -32.18753812416031224, -22.22500000000000142, 4.000000000000000000 ) ) ;
#119350=CARTESIAN_POINT ( 'NONE',  ( 13.36902924655238323, 1.333290112598358945, 4.303104124266152297 ) ) ;
#119352=VECTOR ( 'NONE', #64220, 1000.000000000000000 ) ;
#119353=LINE ( 'NONE', #75886, #20425 ) ;
#119354=LINE ( 'NONE', #9895, #128371 ) ;
#119355=ADVANCED_FACE ( 'NONE', ( #4359 ), #13850, .F. ) ;
#119356=DIRECTION ( 'NONE',  ( -0.6830127018922180770, -0.6830127018922204085, -0.2588190451025213501 ) ) ;
#119357=LINE ( 'NONE', #111348, #85511 ) ;
#119359=VERTEX_POINT ( 'NONE', #91458 ) ;
#119360=DIRECTION ( 'NONE',  ( -0.6830127018922180770, -0.6830127018922204085, -0.2588190451025213501 ) ) ;
#119362=ORIENTED_EDGE ( 'NONE', *, *, #8647, .F. ) ;
#119363=ADVANCED_FACE ( 'NONE', ( #116029 ), #102344, .F. ) ;
#119365=ORIENTED_EDGE ( 'NONE', *, *, #125350, .F. ) ;
#119366=VERTEX_POINT ( 'NONE', #2993 ) ;
#119368=EDGE_LOOP ( 'NONE', ( #32037, #50048, #55357, #139183, #27203 ) ) ;
#119370=ORIENTED_EDGE ( 'NONE', *, *, #86994, .T. ) ;
#119371=ORIENTED_EDGE ( 'NONE', *, *, #136580, .F. ) ;
#119372=VECTOR ( 'NONE', #18556, 999.9999999999998863 ) ;
#119378=VECTOR ( 'NONE', #35473, 999.9999999999998863 ) ;
#119380=ORIENTED_EDGE ( 'NONE', *, *, #135523, .T. ) ;
#119381=CARTESIAN_POINT ( 'NONE',  ( 0.4892135623730947680, -27.52281430457055578, 5.000000000000000000 ) ) ;
#119382=AXIS2_PLACEMENT_3D ( 'NONE', #75104, #130183, #10507 ) ;
#119383=FACE_OUTER_BOUND ( 'NONE', #107450, .T. ) ;
#119384=EDGE_CURVE ( 'NONE', #62368, #39664, #82035, .T. ) ;
#119387=ORIENTED_EDGE ( 'NONE', *, *, #25981, .T. ) ;
#119388=DIRECTION ( 'NONE',  ( 1.000000000000000000, 0.000000000000000000, 0.000000000000000000 ) ) ;
#119389=ORIENTED_EDGE ( 'NONE', *, *, #93391, .T. ) ;
#119390=VERTEX_POINT ( 'NONE', #125510 ) ;
#119391=EDGE_LOOP ( 'NONE', ( #69784, #96216, #133026, #114723 ) ) ;
#119395=LINE ( 'NONE', #77894, #54783 ) ;
#119396=DIRECTION ( 'NONE',  ( -0.7071067811865486830, -0.7071067811865464625, -0.000000000000000000 ) ) ;
#119397=PLANE ( 'NONE',  #32446 ) ;
#119398=ORIENTED_EDGE ( 'NONE', *, *, #40352, .T. ) ;
#119402=PLANE ( 'NONE',  #39302 ) ;
#119403=EDGE_CURVE ( 'NONE', #72122, #58614, #61010, .T. ) ;
#119404=CARTESIAN_POINT ( 'NONE',  ( 34.92499999999998295, 1.512461875839459680, 4.000000000000000000 ) ) ;
#119406=ORIENTED_EDGE ( 'NONE', *, *, #99424, .F. ) ;
#119407=EDGE_CURVE ( 'NONE', #55578, #100010, #92858, .T. ) ;
#119408=ORIENTED_EDGE ( 'NONE', *, *, #38620, .T. ) ;
#119412=CARTESIAN_POINT ( 'NONE',  ( -0.1839886062690032631, 28.73617430169787568, 5.000000000000000000 ) ) ;
#119413=DIRECTION ( 'NONE',  ( 0.7071067811865487940, 0.7071067811865463515, -0.000000000000000000 ) ) ;
#119414=EDGE_CURVE ( 'NONE', #110607, #100364, #36360, .T. ) ;
#119415=EDGE_CURVE ( 'NONE', #54885, #13795, #90753, .T. ) ;
#119419=LINE ( 'NONE', #63672, #71895 ) ;
#119422=CARTESIAN_POINT ( 'NONE',  ( 14.71998032010587565, 0.7592924766157173044, 14.27032725228012033 ) ) ;
#119423=ORIENTED_EDGE ( 'NONE', *, *, #82785, .F. ) ;
#119424=DIRECTION ( 'NONE',  ( 0.6830127018922181881, 0.6830127018922202975, -0.2588190451025214056 ) ) ;
#119425=VERTEX_POINT ( 'NONE', #49405 ) ;
#119426=( BOUNDED_CURVE ( )  B_SPLINE_CURVE ( 3, ( #91929, #134767, #115076, #136155 ),
 .UNSPECIFIED., .F., .T. ) 
 B_SPLINE_CURVE_WITH_KNOTS ( ( 4, 4 ),
 ( 1.378368140454906854, 1.408685637663195767 ),
 .UNSPECIFIED. ) 
 CURVE ( )  GEOMETRIC_REPRESENTATION_ITEM ( )  RATIONAL_B_SPLINE_CURVE ( ( 1.000000000000000000, 0.9999234055803066790, 0.9999234055803066790, 1.000000000000000000 ) ) 
 REPRESENTATION_ITEM ( '' )  );
#119427=CARTESIAN_POINT ( 'NONE',  ( 23.29298673570678346, -21.74070752338406720, 4.999753212805222446 ) ) ;
#119428=CARTESIAN_POINT ( 'NONE',  ( -48.48921356237309510, -27.52281430457089328, 5.000000000000000000 ) ) ;
#119429=ORIENTED_EDGE ( 'NONE', *, *, #65776, .T. ) ;
#119430=ADVANCED_FACE ( 'NONE', ( #26896 ), #79905, .F. ) ;
#119431=EDGE_CURVE ( 'NONE', #57808, #81070, #71140, .T. ) ;
#119432=DIRECTION ( 'NONE',  ( -0.3543493200069162685, -0.000000000000000000, -0.9351131265310288487 ) ) ;
#119433=ORIENTED_EDGE ( 'NONE', *, *, #141852, .T. ) ;
#119434=DIRECTION ( 'NONE',  ( 0.7071067811865487940, 0.7071067811865463515, -0.000000000000000000 ) ) ;
#119436=FACE_OUTER_BOUND ( 'NONE', #30761, .T. ) ;
#119437=ORIENTED_EDGE ( 'NONE', *, *, #109081, .T. ) ;
#119439=VECTOR ( 'NONE', #124694, 1000.000000000000000 ) ;
#119443=CARTESIAN_POINT ( 'NONE',  ( -15.47512612785036090, 14.25929247661557575, 9.797011795316599603 ) ) ;
#119444=CARTESIAN_POINT ( 'NONE',  ( -32.29289321881322650, -3.740707523384248390, 5.000000000000000000 ) ) ;
#119446=CARTESIAN_POINT ( 'NONE',  ( 2.161706124526183714, -6.740707523384205757, 16.75550250614867664 ) ) ;
#119449=ADVANCED_FACE ( 'NONE', ( #113176 ), #47286, .T. ) ;
#119450=CARTESIAN_POINT ( 'NONE',  ( 8.999999999999932498, 20.70535890316562089, 1.956823837851896286 ) ) ;
#119451=PLANE ( 'NONE',  #6149 ) ;
#119452=ORIENTED_EDGE ( 'NONE', *, *, #122190, .T. ) ;
#119453=ORIENTED_EDGE ( 'NONE', *, *, #40880, .T. ) ;
#119454=PLANE ( 'NONE',  #118422 ) ;
#119456=VECTOR ( 'NONE', #30134, 1000.000000000000000 ) ;
#119457=LINE ( 'NONE', #75989, #115060 ) ;
#119460=EDGE_CURVE ( 'NONE', #79224, #55061, #82719, .T. ) ;
#119462=ORIENTED_EDGE ( 'NONE', *, *, #35492, .T. ) ;
#119463=CARTESIAN_POINT ( 'NONE',  ( -0.4892135623730947680, -27.52281430457055578, 5.000000000000000000 ) ) ;
#119465=VECTOR ( 'NONE', #94883, 1000.000000000000000 ) ;
#119467=DIRECTION ( 'NONE',  ( 0.7071067811865487940, 0.7071067811865463515, 0.000000000000000000 ) ) ;
#119468=ORIENTED_EDGE ( 'NONE', *, *, #11334, .T. ) ;
#119469=CARTESIAN_POINT ( 'NONE',  ( 28.17183060077627133, 15.75929247661555443, 4.000000000000000000 ) ) ;
#119470=ADVANCED_FACE ( 'NONE', ( #62403 ), #40645, .F. ) ;
#119472=FACE_OUTER_BOUND ( 'NONE', #127386, .T. ) ;
#119473=VECTOR ( 'NONE', #30000, 1000.000000000000000 ) ;
#119474=CARTESIAN_POINT ( 'NONE',  ( -45.48921356237309510, -27.52281430457087197, 5.000000000000000000 ) ) ;
#119475=ORIENTED_EDGE ( 'NONE', *, *, #72093, .T. ) ;
#119477=ORIENTED_EDGE ( 'NONE', *, *, #40269, .F. ) ;
#119478=ORIENTED_EDGE ( 'NONE', *, *, #122190, .F. ) ;
#119479=AXIS2_PLACEMENT_3D ( 'NONE', #56604, #100770, #45707 ) ;
#119482=VECTOR ( 'NONE', #58032, 1000.000000000000000 ) ;
#119485=CARTESIAN_POINT ( 'NONE',  ( 21.18398860626899349, 28.73617430169802134, 5.000000000000000000 ) ) ;
#119486=VERTEX_POINT ( 'NONE', #50095 ) ;
#119491=CARTESIAN_POINT ( 'NONE',  ( 26.99999999999981881, -1.447814304570811617, 5.000000000000000000 ) ) ;
#119492=CARTESIAN_POINT ( 'NONE',  ( 23.99999999999983302, -12.03360074219761167, 5.000000000000000000 ) ) ;
#119493=DIRECTION ( 'NONE',  ( 0.3543493200069164351, 2.781805975412904658E-17, -0.9351131265310288487 ) ) ;
#119494=FACE_OUTER_BOUND ( 'NONE', #118050, .T. ) ;
#119495=ORIENTED_EDGE ( 'NONE', *, *, #78913, .F. ) ;
#119496=ORIENTED_EDGE ( 'NONE', *, *, #46354, .T. ) ;
#119497=ORIENTED_EDGE ( 'NONE', *, *, #80007, .F. ) ;
#119498=LINE ( 'NONE', #54308, #79260 ) ;
#119499=DIRECTION ( 'NONE',  ( -0.7071067811865486830, -0.7071067811865464625, 0.000000000000000000 ) ) ;
#119501=CARTESIAN_POINT ( 'NONE',  ( -13.17183060077638679, -2.240707523384260824, 4.000000000000000000 ) ) ;
#119502=DIRECTION ( 'NONE',  ( 0.6830127018922180770, -0.6830127018922204085, -0.2588190451025213501 ) ) ;
#119503=ORIENTED_EDGE ( 'NONE', *, *, #5413, .F. ) ;
#119504=EDGE_LOOP ( 'NONE', ( #137225, #100269, #121726, #47918 ) ) ;
#119505=CARTESIAN_POINT ( 'NONE',  ( -21.88339156388719431, -2.079482862307782121, 4.335713449946893228 ) ) ;
#119507=EDGE_CURVE ( 'NONE', #27663, #46917, #96403, .T. ) ;
#119508=EDGE_LOOP ( 'NONE', ( #108611, #109773, #1615, #7172 ) ) ;
#119509=VECTOR ( 'NONE', #99697, 1000.000000000000000 ) ;
#119512=ORIENTED_EDGE ( 'NONE', *, *, #71975, .F. ) ;
#119513=CARTESIAN_POINT ( 'NONE',  ( 34.92499999999998295, 22.22500000000000142, 4.000000000000000000 ) ) ;
#119514=EDGE_CURVE ( 'NONE', #57507, #132762, #118156, .T. ) ;
#119515=PLANE ( 'NONE',  #89548 ) ;
#119516=VECTOR ( 'NONE', #92699, 1000.000000000000000 ) ;
#119517=CARTESIAN_POINT ( 'NONE',  ( -11.99999999999991651, -21.03360074219752462, 5.000000000000000000 ) ) ;
#119518=LINE ( 'NONE', #87641, #51314 ) ;
#119519=ORIENTED_EDGE ( 'NONE', *, *, #126843, .F. ) ;
#119520=ORIENTED_EDGE ( 'NONE', *, *, #137968, .T. ) ;
#119522=ADVANCED_FACE ( 'NONE', ( #31195 ), #63828, .F. ) ;
#119523=DIRECTION ( 'NONE',  ( 0.7071067811865487940, 0.7071067811865463515, 0.000000000000000000 ) ) ;
#119524=ORIENTED_EDGE ( 'NONE', *, *, #125262, .T. ) ;
#119525=PLANE ( 'NONE',  #109321 ) ;
#119526=ORIENTED_EDGE ( 'NONE', *, *, #53007, .F. ) ;
#119528=ADVANCED_FACE ( 'NONE', ( #75412 ), #97103, .F. ) ;
#119529=VERTEX_POINT ( 'NONE', #7975 ) ;
#119530=ORIENTED_EDGE ( 'NONE', *, *, #37258, .T. ) ;
#119531=EDGE_CURVE ( 'NONE', #9882, #3445, #140641, .T. ) ;
#119532=VERTEX_POINT ( 'NONE', #83436 ) ;
#119533=ADVANCED_FACE ( 'NONE', ( #17439 ), #94984, .F. ) ;
#119536=DIRECTION ( 'NONE',  ( -0.7071067811865486830, 0.7071067811865464625, 0.000000000000000000 ) ) ;
#119537=LINE ( 'NONE', #142754, #32193 ) ;
#119538=DIRECTION ( 'NONE',  ( 0.000000000000000000, -1.000000000000000000, 0.000000000000000000 ) ) ;
#119539=VECTOR ( 'NONE', #121489, 1000.000000000000000 ) ;
#119541=FACE_OUTER_BOUND ( 'NONE', #37588, .T. ) ;
#119542=ADVANCED_FACE ( 'NONE', ( #127649 ), #28341, .T. ) ;
#119543=CARTESIAN_POINT ( 'NONE',  ( -27.79289321881326202, -17.24070752338409918, 5.000000000000000000 ) ) ;
#119544=DIRECTION ( 'NONE',  ( -0.7071067811865486830, 0.7071067811865464625, 0.000000000000000000 ) ) ;
#119545=DIRECTION ( 'NONE',  ( -0.7071067811865486830, 0.7071067811865464625, 0.000000000000000000 ) ) ;
#119546=EDGE_CURVE ( 'NONE', #118475, #127411, #32662, .T. ) ;
#119547=PLANE ( 'NONE',  #59829 ) ;
#119548=DIRECTION ( 'NONE',  ( -0.7071067811865486830, -0.7071067811865464625, 0.000000000000000000 ) ) ;
#119549=LINE ( 'NONE', #142764, #37836 ) ;
#119551=ORIENTED_EDGE ( 'NONE', *, *, #135943, .T. ) ;
#119552=ORIENTED_EDGE ( 'NONE', *, *, #106887, .T. ) ;
#119553=ORIENTED_EDGE ( 'NONE', *, *, #119704, .F. ) ;
#119554=ORIENTED_EDGE ( 'NONE', *, *, #2424, .F. ) ;
#119555=DIRECTION ( 'NONE',  ( 0.6830127018922181881, 0.6830127018922202975, -0.2588190451025214056 ) ) ;
#119556=EDGE_CURVE ( 'NONE', #33921, #38622, #50798, .T. ) ;
#119557=VERTEX_POINT ( 'NONE', #18119 ) ;
#119558=ORIENTED_EDGE ( 'NONE', *, *, #68335, .F. ) ;
#119559=LINE ( 'NONE', #128347, #125518 ) ;
#119560=CARTESIAN_POINT ( 'NONE',  ( 8.994519915287490619, 28.92564299267944250, 4.000000000000000000 ) ) ;
#119561=AXIS2_PLACEMENT_3D ( 'NONE', #23599, #24318, #45391 ) ;
#119562=LINE ( 'NONE', #51504, #18433 ) ;
#119563=ORIENTED_EDGE ( 'NONE', *, *, #121194, .T. ) ;
#119564=CARTESIAN_POINT ( 'NONE',  ( 24.07469600201484283, -0.04978799960961742543, 4.760162856047378099 ) ) ;
#119565=EDGE_CURVE ( 'NONE', #133408, #123203, #52216, .T. ) ;
#119566=ADVANCED_FACE ( 'NONE', ( #106565 ), #128369, .F. ) ;
#119569=VECTOR ( 'NONE', #122006, 999.9999999999998863 ) ;
#119570=CARTESIAN_POINT ( 'NONE',  ( 31.49999999999977973, 13.46639925780212010, 5.000000000000000000 ) ) ;
#119571=CARTESIAN_POINT ( 'NONE',  ( -14.99999999999988098, -19.44781430457063465, 5.000000000000000000 ) ) ;
#119572=VECTOR ( 'NONE', #83878, 1000.000000000000000 ) ;
#119577=LINE ( 'NONE', #131928, #60640 ) ;
#119578=ORIENTED_EDGE ( 'NONE', *, *, #125672, .F. ) ;
#119579=EDGE_CURVE ( 'NONE', #132258, #134235, #51524, .T. ) ;
#119580=VERTEX_POINT ( 'NONE', #95718 ) ;
#119582=ORIENTED_EDGE ( 'NONE', *, *, #107516, .F. ) ;
#119583=CARTESIAN_POINT ( 'NONE',  ( -3.183988606268992161, 28.73617430169789699, 5.000000000000000000 ) ) ;
#119584=CARTESIAN_POINT ( 'NONE',  ( -19.27928215921719612, -2.789594763390444321, 4.000000000000000000 ) ) ;
#119586=DIRECTION ( 'NONE',  ( 0.6830127018922180770, -0.6830127018922204085, -0.2588190451025213501 ) ) ;
#119587=CARTESIAN_POINT ( 'NONE',  ( 24.32816939922335919, -3.740707523384244837, 4.000000000000000000 ) ) ;
#119588=EDGE_LOOP ( 'NONE', ( #74991, #90038, #91022, #67956 ) ) ;
#119589=ADVANCED_FACE ( 'NONE', ( #139970 ), #30476, .F. ) ;
#119590=EDGE_CURVE ( 'NONE', #64185, #141627, #109451, .T. ) ;
#119591=LINE ( 'NONE', #20286, #36787 ) ;
#119593=DIRECTION ( 'NONE',  ( 0.7071067811865487940, 0.7071067811865463515, -0.000000000000000000 ) ) ;
#119594=VERTEX_POINT ( 'NONE', #111596 ) ;
#119595=DIRECTION ( 'NONE',  ( -0.6830127018922180770, -0.6830127018922204085, -0.2588190451025214056 ) ) ;
#119596=LINE ( 'NONE', #11543, #81825 ) ;
#119597=EDGE_CURVE ( 'NONE', #84015, #46769, #89830, .T. ) ;
#119598=ORIENTED_EDGE ( 'NONE', *, *, #83540, .T. ) ;
#119599=CARTESIAN_POINT ( 'NONE',  ( -32.99451991528749062, 28.92564299267960948, 4.000000000000000000 ) ) ;
#119601=EDGE_CURVE ( 'NONE', #16081, #89139, #121737, .T. ) ;
#119602=ORIENTED_EDGE ( 'NONE', *, *, #46571, .T. ) ;
#119604=CARTESIAN_POINT ( 'NONE',  ( -34.92500000000001137, 3.006123077391908094, 4.000000000000000000 ) ) ;
#119605=ORIENTED_EDGE ( 'NONE', *, *, #100917, .T. ) ;
#119606=CARTESIAN_POINT ( 'NONE',  ( 26.99451991528749417, 28.92564299267956685, 4.000000000000000000 ) ) ;
#119607=DIRECTION ( 'NONE',  ( -0.000000000000000000, 0.000000000000000000, 1.000000000000000000 ) ) ;
#119608=EDGE_CURVE ( 'NONE', #114524, #53240, #42831, .T. ) ;
#119609=DIRECTION ( 'NONE',  ( 1.000000000000000000, 0.000000000000000000, 0.000000000000000000 ) ) ;
#119610=CARTESIAN_POINT ( 'NONE',  ( -33.75860074219772855, 21.72500000000000142, 5.000000000000000000 ) ) ;
#119611=DIRECTION ( 'NONE',  ( -0.7071067811865486830, 0.7071067811865464625, 0.000000000000000000 ) ) ;
#119612=CARTESIAN_POINT ( 'NONE',  ( 2.994519915287485734, 28.92564299267940342, 4.000000000000000000 ) ) ;
#119615=FACE_OUTER_BOUND ( 'NONE', #24676, .T. ) ;
#119617=PLANE ( 'NONE',  #96911 ) ;
#119618=EDGE_CURVE ( 'NONE', #69925, #123496, #79000, .T. ) ;
#119619=CARTESIAN_POINT ( 'NONE',  ( -26.99999999999980815, 20.96639925780204550, 5.000000000000000000 ) ) ;
#119620=CARTESIAN_POINT ( 'NONE',  ( -34.92500000000001137, 14.93779483949078823, 7.761394445350714655 ) ) ;
#119621=ORIENTED_EDGE ( 'NONE', *, *, #141574, .T. ) ;
#119622=VERTEX_POINT ( 'NONE', #134074 ) ;
#119623=ORIENTED_EDGE ( 'NONE', *, *, #102662, .T. ) ;
#119626=ORIENTED_EDGE ( 'NONE', *, *, #9833, .T. ) ;
#119627=EDGE_LOOP ( 'NONE', ( #27225, #73361, #2736, #17631 ) ) ;
#119629=CARTESIAN_POINT ( 'NONE',  ( 18.48921356237309510, -27.52281430457068367, 5.000000000000000000 ) ) ;
#119630=CARTESIAN_POINT ( 'NONE',  ( -13.17183060077637613, 0.7592924766157069794, 4.000000000000000000 ) ) ;
#119631=ORIENTED_EDGE ( 'NONE', *, *, #120122, .T. ) ;
#119632=PLANE ( 'NONE',  #25427 ) ;
#119635=CARTESIAN_POINT ( 'NONE',  ( -23.99999999999982947, 19.93112307739197675, 4.000000000000000000 ) ) ;
#119637=VERTEX_POINT ( 'NONE', #76120 ) ;
#119638=FACE_OUTER_BOUND ( 'NONE', #30016, .T. ) ;
#119639=CARTESIAN_POINT ( 'NONE',  ( -31.49999999999977973, -7.533600742197658739, 5.000000000000000000 ) ) ;
#119640=LINE ( 'NONE', #142167, #49795 ) ;
#119641=DIRECTION ( 'NONE',  ( 0.000000000000000000, -1.000000000000000000, 0.000000000000000000 ) ) ;
#119642=PLANE ( 'NONE',  #128718 ) ;
#119644=AXIS2_PLACEMENT_3D ( 'NONE', #124921, #13277, #24886 ) ;
#119645=DIRECTION ( 'NONE',  ( 0.7071067811865487940, 0.7071067811865463515, 0.000000000000000000 ) ) ;
#119646=ADVANCED_FACE ( 'NONE', ( #1374 ), #64522, .F. ) ;
#119647=ORIENTED_EDGE ( 'NONE', *, *, #62250, .F. ) ;
#119648=EDGE_LOOP ( 'NONE', ( #77194, #126838, #59462, #43402, #85902 ) ) ;
#119650=AXIS2_PLACEMENT_3D ( 'NONE', #98161, #42370, #62690 ) ;
#119651=ORIENTED_EDGE ( 'NONE', *, *, #138569, .F. ) ;
#119653=CARTESIAN_POINT ( 'NONE',  ( 28.82816939922332722, 18.75929247661552424, 4.000000000000000000 ) ) ;
#119654=LINE ( 'NONE', #132745, #131304 ) ;
#119655=PLANE ( 'NONE',  #104770 ) ;
#119656=LINE ( 'NONE', #20353, #106781 ) ;
#119657=LINE ( 'NONE', #142183, #23315 ) ;
#119659=EDGE_LOOP ( 'NONE', ( #39344, #35054, #73775, #4284 ) ) ;
#119661=CARTESIAN_POINT ( 'NONE',  ( 0.000000000000000000, 0.000000000000000000, 5.000000000000000000 ) ) ;
#119663=LINE ( 'NONE', #57162, #92991 ) ;
#119664=DIRECTION ( 'NONE',  ( -0.3543493200069162685, -0.000000000000000000, -0.9351131265310288487 ) ) ;
#119665=VERTEX_POINT ( 'NONE', #55087 ) ;
#119668=ORIENTED_EDGE ( 'NONE', *, *, #142972, .T. ) ;
#119669=DIRECTION ( 'NONE',  ( -0.7071067811865486830, -0.7071067811865464625, 0.000000000000000000 ) ) ;
#119672=VECTOR ( 'NONE', #68416, 1000.000000000000000 ) ;
#119673=AXIS2_PLACEMENT_3D ( 'NONE', #29811, #105244, #62468 ) ;
#119675=EDGE_LOOP ( 'NONE', ( #46436, #68189, #60157, #42587 ) ) ;
#119676=VECTOR ( 'NONE', #86888, 1000.000000000000000 ) ;
#119678=VERTEX_POINT ( 'NONE', #9385 ) ;
#119679=EDGE_CURVE ( 'NONE', #136567, #58719, #122453, .T. ) ;
#119680=ORIENTED_EDGE ( 'NONE', *, *, #11227, .T. ) ;
#119682=EDGE_LOOP ( 'NONE', ( #77665, #4489, #72636, #107774 ) ) ;
#119684=ORIENTED_EDGE ( 'NONE', *, *, #130466, .F. ) ;
#119686=PLANE ( 'NONE',  #84896 ) ;
#119687=CARTESIAN_POINT ( 'NONE',  ( 14.29289321881335439, 20.25929247661551713, 5.000000000000000000 ) ) ;
#119688=CARTESIAN_POINT ( 'NONE',  ( 26.67183060077628198, -21.74070752338406365, 4.000000000000000000 ) ) ;
#119689=EDGE_CURVE ( 'NONE', #17718, #123774, #76862, .T. ) ;
#119690=FACE_BOUND ( 'NONE', #77259, .T. ) ;
#119691=ORIENTED_EDGE ( 'NONE', *, *, #125635, .T. ) ;
#119693=EDGE_CURVE ( 'NONE', #35104, #108780, #142797, .T. ) ;
#119694=ADVANCED_FACE ( 'NONE', ( #44968 ), #42797, .F. ) ;
#119696=CARTESIAN_POINT ( 'NONE',  ( -13.49999999999991118, -2.568876922607790103, 4.000000000000000000 ) ) ;
#119697=VERTEX_POINT ( 'NONE', #131210 ) ;
#119698=CARTESIAN_POINT ( 'NONE',  ( -21.12147316337133773, -20.24070752338407786, 7.412974875817839759 ) ) ;
#119699=ORIENTED_EDGE ( 'NONE', *, *, #22328, .F. ) ;
#119700=VECTOR ( 'NONE', #55234, 1000.000000000000000 ) ;
#119701=VERTEX_POINT ( 'NONE', #131939 ) ;
#119702=DIRECTION ( 'NONE',  ( -0.7071067811865486830, 0.7071067811865464625, 0.000000000000000000 ) ) ;
#119703=ORIENTED_EDGE ( 'NONE', *, *, #132401, .T. ) ;
#119704=EDGE_CURVE ( 'NONE', #132626, #76656, #107579, .T. ) ;
#119705=ADVANCED_FACE ( 'NONE', ( #110147 ), #676, .F. ) ;
#119707=DIRECTION ( 'NONE',  ( -0.6830127018922181881, 0.6830127018922202975, -0.2588190451025214056 ) ) ;
#119708=VECTOR ( 'NONE', #60389, 1000.000000000000000 ) ;
#119709=EDGE_LOOP ( 'NONE', ( #9667, #101517, #54700, #65049 ) ) ;
#119710=LINE ( 'NONE', #63268, #74187 ) ;
#119711=VERTEX_POINT ( 'NONE', #89144 ) ;
#119712=LINE ( 'NONE', #142925, #24154 ) ;
#119713=EDGE_CURVE ( 'NONE', #133506, #104226, #121035, .T. ) ;
#119714=ORIENTED_EDGE ( 'NONE', *, *, #41148, .F. ) ;
#119715=FACE_OUTER_BOUND ( 'NONE', #33978, .T. ) ;
#119716=CARTESIAN_POINT ( 'NONE',  ( -8.999999999999937828, -0.2811185226894407085, -5.995736974527494212 ) ) ;
#119717=VECTOR ( 'NONE', #38226, 1000.000000000000000 ) ;
#119718=EDGE_CURVE ( 'NONE', #60604, #59118, #34057, .T. ) ;
#119719=CARTESIAN_POINT ( 'NONE',  ( -0.005480084712502889671, 28.92564299267938210, 4.000000000000000000 ) ) ;
#119720=CARTESIAN_POINT ( 'NONE',  ( 23.99999999999982947, 10.21212019023810846, -2.019456568337855362 ) ) ;
#119721=CARTESIAN_POINT ( 'NONE',  ( 18.18398860626898994, 28.73617430169800002, 5.000000000000000000 ) ) ;
#119722=DIRECTION ( 'NONE',  ( -0.7071067811865486830, -0.7071067811865464625, 0.000000000000000000 ) ) ;
#119723=PLANE ( 'NONE',  #64969 ) ;
#119724=ORIENTED_EDGE ( 'NONE', *, *, #134001, .F. ) ;
#119725=AXIS2_PLACEMENT_3D ( 'NONE', #89874, #80465, #34809 ) ;
#119726=ORIENTED_EDGE ( 'NONE', *, *, #99595, .T. ) ;
#119727=VERTEX_POINT ( 'NONE', #35505 ) ;
#119729=DIRECTION ( 'NONE',  ( -0.7071067811865486830, 0.7071067811865464625, 0.000000000000000000 ) ) ;
#119731=EDGE_LOOP ( 'NONE', ( #107996, #112328, #108195, #122969 ) ) ;
#119732=CARTESIAN_POINT ( 'NONE',  ( 9.707106781186482181, -6.740707523384216415, 5.000000000000000000 ) ) ;
#119733=DIRECTION ( 'NONE',  ( 0.7071067811865486830, -0.7071067811865464625, -0.000000000000000000 ) ) ;
#119734=VECTOR ( 'NONE', #35443, 1000.000000000000227 ) ;
#119735=DIRECTION ( 'NONE',  ( -0.3543493200069162685, -0.000000000000000000, -0.9351131265310288487 ) ) ;
#119736=EDGE_LOOP ( 'NONE', ( #19283, #6309, #61731 ) ) ;
#119737=LINE ( 'NONE', #63295, #125028 ) ;
#119738=EDGE_CURVE ( 'NONE', #103456, #38684, #93410, .T. ) ;
#119739=DIRECTION ( 'NONE',  ( 0.7071067811865487940, 0.7071067811865463515, 0.000000000000000000 ) ) ;
#119741=CARTESIAN_POINT ( 'NONE',  ( 3.299744871391591339, -27.71228299555208352, 4.000000000000000000 ) ) ;
#119742=ORIENTED_EDGE ( 'NONE', *, *, #97396, .T. ) ;
#119744=VECTOR ( 'NONE', #95831, 999.9999999999998863 ) ;
#119747=EDGE_CURVE ( 'NONE', #98330, #95580, #79738, .T. ) ;
#119748=CARTESIAN_POINT ( 'NONE',  ( -9.183988606268997046, 28.73617430169793607, 5.000000000000000000 ) ) ;
#119750=VERTEX_POINT ( 'NONE', #136912 ) ;
#119752=ORIENTED_EDGE ( 'NONE', *, *, #130114, .F. ) ;
#119753=CARTESIAN_POINT ( 'NONE',  ( -12.48921356237309155, -27.52281430457064104, 5.000000000000000000 ) ) ;
#119755=CARTESIAN_POINT ( 'NONE',  ( -48.29974487139158867, -27.71228299555239971, 4.000000000000000000 ) ) ;
#119756=VERTEX_POINT ( 'NONE', #38324 ) ;
#119757=EDGE_CURVE ( 'NONE', #60486, #2943, #114440, .T. ) ;
#119758=AXIS2_PLACEMENT_3D ( 'NONE', #40182, #5347, #6043 ) ;
#119759=EDGE_CURVE ( 'NONE', #53860, #101990, #47114, .T. ) ;
#119760=CARTESIAN_POINT ( 'NONE',  ( -28.49999999999979750, 15.05218569542901186, 5.000000000000000000 ) ) ;
#119761=LINE ( 'NONE', #43660, #93049 ) ;
#119762=ORIENTED_EDGE ( 'NONE', *, *, #8486, .T. ) ;
#119764=VECTOR ( 'NONE', #22219, 999.9999999999998863 ) ;
#119765=DIRECTION ( 'NONE',  ( -0.7071067811865486830, 0.7071067811865464625, 0.000000000000000000 ) ) ;
#119766=EDGE_CURVE ( 'NONE', #107904, #28826, #123922, .T. ) ;
#119769=VECTOR ( 'NONE', #113468, 1000.000000000000000 ) ;
#119773=LINE ( 'NONE', #76314, #28764 ) ;
#119774=LINE ( 'NONE', #108899, #69131 ) ;
#119776=VECTOR ( 'NONE', #115051, 1000.000000000000000 ) ;
#119777=DIRECTION ( 'NONE',  ( 0.7071067811865486830, -0.7071067811865464625, -0.000000000000000000 ) ) ;
#119778=AXIS2_PLACEMENT_3D ( 'NONE', #95066, #52283, #126980 ) ;
#119779=CARTESIAN_POINT ( 'NONE',  ( -26.51078643762690845, -27.52281430457036748, 5.000000000000000000 ) ) ;
#119780=DIRECTION ( 'NONE',  ( 0.7071067811865487940, 0.7071067811865463515, 0.000000000000000000 ) ) ;
#119781=ORIENTED_EDGE ( 'NONE', *, *, #66822, .F. ) ;
#119782=ADVANCED_FACE ( 'NONE', ( #36191 ), #82539, .T. ) ;
#119784=DIRECTION ( 'NONE',  ( 0.7071067811865486830, -0.7071067811865464625, -0.000000000000000000 ) ) ;
#119785=CARTESIAN_POINT ( 'NONE',  ( 36.18398860626899705, 28.73617430169812437, 5.000000000000000000 ) ) ;
#119786=VECTOR ( 'NONE', #89053, 1000.000000000000000 ) ;
#119787=DIRECTION ( 'NONE',  ( 0.7071067811865487940, 0.7071067811865463515, -0.000000000000000000 ) ) ;
#119789=DIRECTION ( 'NONE',  ( -0.7071067811865487940, 0.7071067811865463515, -0.000000000000000000 ) ) ;
#119790=ORIENTED_EDGE ( 'NONE', *, *, #107205, .F. ) ;
#119791=ORIENTED_EDGE ( 'NONE', *, *, #31102, .F. ) ;
#119792=CARTESIAN_POINT ( 'NONE',  ( -18.71230993966015177, -21.73547319004781286, 4.999917730833664642 ) ) ;
#119793=ADVANCED_FACE ( 'NONE', ( #135506 ), #14425, .F. ) ;
#119794=ORIENTED_EDGE ( 'NONE', *, *, #24690, .T. ) ;
#119795=VERTEX_POINT ( 'NONE', #70285 ) ;
#119796=LINE ( 'NONE', #19790, #126570 ) ;
#119797=DIRECTION ( 'NONE',  ( -0.000000000000000000, -0.3543493200069152693, 0.9351131265310292928 ) ) ;
#119798=ORIENTED_EDGE ( 'NONE', *, *, #95639, .T. ) ;
#119799=CARTESIAN_POINT ( 'NONE',  ( -17.57538274164440040, -2.608983483842240325, 5.000000000000000000 ) ) ;
#119800=CARTESIAN_POINT ( 'NONE',  ( -14.99999999999989164, -15.41253812416060143, 4.000000000000000000 ) ) ;
#119801=DIRECTION ( 'NONE',  ( -0.000000000000000000, -0.3543493200069152693, 0.9351131265310292928 ) ) ;
#119802=EDGE_CURVE ( 'NONE', #54989, #9815, #60086, .T. ) ;
#119803=FACE_OUTER_BOUND ( 'NONE', #120433, .T. ) ;
#119805=VERTEX_POINT ( 'NONE', #81127 ) ;
#119806=DIRECTION ( 'NONE',  ( -0.7071067811865486830, -0.7071067811865464625, 0.000000000000000000 ) ) ;
#119807=FACE_OUTER_BOUND ( 'NONE', #43432, .T. ) ;
#119808=AXIS2_PLACEMENT_3D ( 'NONE', #79352, #25621, #3152 ) ;
#119809=FACE_OUTER_BOUND ( 'NONE', #61362, .T. ) ;
#119811=CARTESIAN_POINT ( 'NONE',  ( 32.20710678118632586, -14.24070752338414181, 5.000000000000000000 ) ) ;
#119812=LINE ( 'NONE', #163, #14409 ) ;
#119813=CARTESIAN_POINT ( 'NONE',  ( -39.48921356237310221, -27.52281430457082934, 5.000000000000000000 ) ) ;
#119815=EDGE_CURVE ( 'NONE', #133491, #107648, #101425, .T. ) ;
#119816=PLANE ( 'NONE',  #97006 ) ;
#119817=ORIENTED_EDGE ( 'NONE', *, *, #79802, .T. ) ;
#119818=ORIENTED_EDGE ( 'NONE', *, *, #87534, .T. ) ;
#119820=PLANE ( 'NONE',  #118792 ) ;
#119821=DIRECTION ( 'NONE',  ( 0.3543493200069162685, -0.000000000000000000, -0.9351131265310288487 ) ) ;
#119822=CARTESIAN_POINT ( 'NONE',  ( 20.29320749275913371, 20.25929247661551358, 20.83292124670810352 ) ) ;
#119824=CARTESIAN_POINT ( 'NONE',  ( -33.32816939922329880, -6.740707523384212863, 4.000000000000000000 ) ) ;
#119825=( BOUNDED_CURVE ( )  B_SPLINE_CURVE ( 3, ( #91776, #34558, #69335, #101948 ),
 .UNSPECIFIED., .F., .F. ) 
 B_SPLINE_CURVE_WITH_KNOTS ( ( 4, 4 ),
 ( 1.964434688349490754, 3.503810798801452187 ),
 .UNSPECIFIED. ) 
 CURVE ( )  GEOMETRIC_REPRESENTATION_ITEM ( )  RATIONAL_B_SPLINE_CURVE ( ( 1.000000000000000000, 0.8120851936182287290, 0.8120851936182287290, 1.000000000000000000 ) ) 
 REPRESENTATION_ITEM ( '' )  );
#119826=CARTESIAN_POINT ( 'NONE',  ( 75.29974487139158157, -27.71228299555258445, 4.000000000000000000 ) ) ;
#119827=EDGE_CURVE ( 'NONE', #60723, #68187, #80420, .T. ) ;
#119829=ORIENTED_EDGE ( 'NONE', *, *, #54508, .T. ) ;
#119830=EDGE_LOOP ( 'NONE', ( #35891, #82490, #129419, #211 ) ) ;
#119831=ORIENTED_EDGE ( 'NONE', *, *, #36040, .T. ) ;
#119832=DIRECTION ( 'NONE',  ( -0.7071067811865486830, -0.7071067811865464625, 0.000000000000000000 ) ) ;
#119833=CARTESIAN_POINT ( 'NONE',  ( 26.99999999999981526, 4.552185695429121104, 5.000000000000000000 ) ) ;
#119834=CARTESIAN_POINT ( 'NONE',  ( -33.32816939922329880, 17.25929247661554200, 4.000000000000000000 ) ) ;
#119836=ORIENTED_EDGE ( 'NONE', *, *, #107384, .T. ) ;
#119837=EDGE_CURVE ( 'NONE', #489, #72622, #58704, .T. ) ;
#119838=DIRECTION ( 'NONE',  ( 0.6830127018922181881, 0.6830127018922202975, -0.2588190451025214056 ) ) ;
#119840=ORIENTED_EDGE ( 'NONE', *, *, #64471, .F. ) ;
#119842=LINE ( 'NONE', #87253, #97113 ) ;
#119845=VERTEX_POINT ( 'NONE', #124609 ) ;
#119846=VECTOR ( 'NONE', #25772, 1000.000000000000000 ) ;
#119849=DIRECTION ( 'NONE',  ( -0.7071067811865486830, -0.7071067811865464625, 0.000000000000000000 ) ) ;
#119850=CARTESIAN_POINT ( 'NONE',  ( -27.70701326429286127, -21.74070752338406365, 4.999753212805221558 ) ) ;
#119851=PLANE ( 'NONE',  #31645 ) ;
#119852=ORIENTED_EDGE ( 'NONE', *, *, #19840, .T. ) ;
#119853=EDGE_LOOP ( 'NONE', ( #53524, #103264, #130425, #106664 ) ) ;
#119856=EDGE_LOOP ( 'NONE', ( #54569, #47611, #27932, #131946, #46646, #30122, #108651, #133782 ) ) ;
#119857=ORIENTED_EDGE ( 'NONE', *, *, #28321, .F. ) ;
#119858=VECTOR ( 'NONE', #123454, 1000.000000000000000 ) ;
#119860=ORIENTED_EDGE ( 'NONE', *, *, #61142, .T. ) ;
#119862=ADVANCED_FACE ( 'NONE', ( #90571 ), #46386, .F. ) ;
#119863=DIRECTION ( 'NONE',  ( 0.6830127018922181881, 0.6830127018922202975, -0.2588190451025214056 ) ) ;
#119864=VECTOR ( 'NONE', #69168, 999.9999999999998863 ) ;
#119865=FACE_OUTER_BOUND ( 'NONE', #83601, .T. ) ;
#119867=FACE_BOUND ( 'NONE', #56567, .T. ) ;
#119868=EDGE_CURVE ( 'NONE', #103662, #28826, #47803, .T. ) ;
#119869=CARTESIAN_POINT ( 'NONE',  ( 19.05000000000000071, 3.174999999999997158, 4.000000000000000000 ) ) ;
#119870=PLANE ( 'NONE',  #73464 ) ;
#119871=CARTESIAN_POINT ( 'NONE',  ( 9.489213562373095101, -27.52281430457062328, 5.000000000000000000 ) ) ;
#119872=ORIENTED_EDGE ( 'NONE', *, *, #33578, .F. ) ;
#119873=AXIS2_PLACEMENT_3D ( 'NONE', #127051, #27743, #52350 ) ;
#119874=AXIS2_PLACEMENT_3D ( 'NONE', #53032, #6640, #63260 ) ;
#119875=ORIENTED_EDGE ( 'NONE', *, *, #1413, .T. ) ;
#119876=EDGE_CURVE ( 'NONE', #38905, #134825, #113006, .T. ) ;
#119877=EDGE_CURVE ( 'NONE', #64329, #110885, #91977, .T. ) ;
#119878=ORIENTED_EDGE ( 'NONE', *, *, #27472, .T. ) ;
#119881=PLANE ( 'NONE',  #24505 ) ;
#119882=EDGE_CURVE ( 'NONE', #80880, #58909, #103545, .T. ) ;
#119883=FACE_OUTER_BOUND ( 'NONE', #70754, .T. ) ;
#119884=ADVANCED_FACE ( 'NONE', ( #48473 ), #15790, .F. ) ;
#119886=DIRECTION ( 'NONE',  ( 0.7071067811865487940, -0.7071067811865463515, 0.000000000000000000 ) ) ;
#119887=EDGE_CURVE ( 'NONE', #32826, #115089, #52054, .T. ) ;
#119889=LINE ( 'NONE', #8269, #39182 ) ;
#119891=FACE_OUTER_BOUND ( 'NONE', #5224, .T. ) ;
#119892=DIRECTION ( 'NONE',  ( 0.7071067811865487940, -0.7071067811865463515, 0.000000000000000000 ) ) ;
#119893=CARTESIAN_POINT ( 'NONE',  ( 8.999999999999937828, 5.587461875839188075, 4.000000000000000000 ) ) ;
#119895=ORIENTED_EDGE ( 'NONE', *, *, #131351, .T. ) ;
#119896=LINE ( 'NONE', #96709, #19115 ) ;
#119898=DIRECTION ( 'NONE',  ( -0.7071067811865487940, 0.7071067811865463515, 0.000000000000000000 ) ) ;
#119900=EDGE_CURVE ( 'NONE', #30706, #55488, #6344, .T. ) ;
#119901=ORIENTED_EDGE ( 'NONE', *, *, #83819, .T. ) ;
#119902=VERTEX_POINT ( 'NONE', #39770 ) ;
#119905=VECTOR ( 'NONE', #89957, 1000.000000000000227 ) ;
#119906=EDGE_LOOP ( 'NONE', ( #12757, #59178, #39069, #42613 ) ) ;
#119907=CARTESIAN_POINT ( 'NONE',  ( 2.999999999999985345, -12.03360074219761877, 5.000000000000000000 ) ) ;
#119908=EDGE_CURVE ( 'NONE', #76199, #138835, #71668, .T. ) ;
#119909=PLANE ( 'NONE',  #35477 ) ;
#119912=ORIENTED_EDGE ( 'NONE', *, *, #129122, .T. ) ;
#119913=VERTEX_POINT ( 'NONE', #73799 ) ;
#119915=CARTESIAN_POINT ( 'NONE',  ( -10.22850677138658426, 20.25929247661551003, 7.808871592221746205 ) ) ;
#119917=DIRECTION ( 'NONE',  ( 0.7071067811865486830, -0.7071067811865464625, -0.000000000000000000 ) ) ;
#119918=ORIENTED_EDGE ( 'NONE', *, *, #72367, .T. ) ;
#119919=ORIENTED_EDGE ( 'NONE', *, *, #133768, .T. ) ;
#119920=LINE ( 'NONE', #87339, #119087 ) ;
#119921=PLANE ( 'NONE',  #109320 ) ;
#119922=ORIENTED_EDGE ( 'NONE', *, *, #14467, .F. ) ;
#119923=CARTESIAN_POINT ( 'NONE',  ( 3.792893218813436551, 18.75929247661553489, 5.000000000000000000 ) ) ;
#119925=ORIENTED_EDGE ( 'NONE', *, *, #31276, .T. ) ;
#119927=EDGE_CURVE ( 'NONE', #962, #44445, #50620, .T. ) ;
#119928=PLANE ( 'NONE',  #70332 ) ;
#119929=LINE ( 'NONE', #21373, #9314 ) ;
#119930=CARTESIAN_POINT ( 'NONE',  ( -26.47234709111790707, 22.22500000000000142, 1.796973836066164898 ) ) ;
#119931=EDGE_CURVE ( 'NONE', #109110, #98525, #83998, .T. ) ;
#119932=DIRECTION ( 'NONE',  ( 0.3543493200069163240, -0.000000000000000000, 0.9351131265310288487 ) ) ;
#119933=LINE ( 'NONE', #32259, #100373 ) ;
#119935=ORIENTED_EDGE ( 'NONE', *, *, #84472, .F. ) ;
#119937=ORIENTED_EDGE ( 'NONE', *, *, #18450, .F. ) ;
#119938=LINE ( 'NONE', #130882, #794 ) ;
#119939=ADVANCED_FACE ( 'NONE', ( #27414 ), #39027, .F. ) ;
#119940=CARTESIAN_POINT ( 'NONE',  ( 34.92499999999998295, 22.22500000000000142, 4.500000000000000888 ) ) ;
#119941=ORIENTED_EDGE ( 'NONE', *, *, #2710, .T. ) ;
#119942=FACE_OUTER_BOUND ( 'NONE', #6070, .T. ) ;
#119943=VECTOR ( 'NONE', #101740, 1000.000000000000000 ) ;
#119944=DIRECTION ( 'NONE',  ( 1.000000000000000000, 0.000000000000000000, 0.000000000000000000 ) ) ;
#119946=ORIENTED_EDGE ( 'NONE', *, *, #131252, .F. ) ;
#119948=DIRECTION ( 'NONE',  ( 1.000000000000000000, 0.000000000000000000, 0.000000000000000000 ) ) ;
#119949=CARTESIAN_POINT ( 'NONE',  ( -29.22995720542185794, 21.73644205237998150, 5.000000000000000000 ) ) ;
#119950=LINE ( 'NONE', #140316, #77091 ) ;
#119952=CARTESIAN_POINT ( 'NONE',  ( 9.989119713460446803, -22.02621442084247505, 4.990779571109222879 ) ) ;
#119954=CARTESIAN_POINT ( 'NONE',  ( 0.000000000000000000, 0.000000000000000000, 5.000000000000000000 ) ) ;
#119955=DIRECTION ( 'NONE',  ( 0.7071067811865486830, -0.7071067811865464625, -0.000000000000000000 ) ) ;
#119956=LINE ( 'NONE', #75098, #67288 ) ;
#119958=ORIENTED_EDGE ( 'NONE', *, *, #105298, .F. ) ;
#119960=EDGE_LOOP ( 'NONE', ( #68257, #61554, #43672, #34071 ) ) ;
#119961=CARTESIAN_POINT ( 'NONE',  ( 24.18398860626899705, 28.73617430169804265, 5.000000000000000000 ) ) ;
#119962=DIRECTION ( 'NONE',  ( 0.7071067811865486830, -0.7071067811865464625, -0.000000000000000000 ) ) ;
#119963=ORIENTED_EDGE ( 'NONE', *, *, #143392, .T. ) ;
#119964=VECTOR ( 'NONE', #58471, 1000.000000000000000 ) ;
#119966=CARTESIAN_POINT ( 'NONE',  ( 5.306730066903978305, -3.740707523384244837, 12.88036043432866329 ) ) ;
#119967=CARTESIAN_POINT ( 'NONE',  ( 45.29974487139158867, -27.71228299555237840, 4.000000000000000000 ) ) ;
#119969=VECTOR ( 'NONE', #86754, 1000.000000000000000 ) ;
#119971=EDGE_CURVE ( 'NONE', #58745, #13885, #128881, .T. ) ;
#119972=CARTESIAN_POINT ( 'NONE',  ( -36.29974487139159578, -27.71228299555231445, 4.000000000000000000 ) ) ;
#119973=LINE ( 'NONE', #64931, #119000 ) ;
#119974=VERTEX_POINT ( 'NONE', #18674 ) ;
#119976=DIRECTION ( 'NONE',  ( -0.7071067811865486830, -0.7071067811865464625, -0.000000000000000000 ) ) ;
#119977=CARTESIAN_POINT ( 'NONE',  ( -36.18398860626899705, 28.73617430169812437, 5.000000000000000000 ) ) ;
#119978=VECTOR ( 'NONE', #86239, 1000.000000000000000 ) ;
#119979=LINE ( 'NONE', #139665, #75418 ) ;
#119981=DIRECTION ( 'NONE',  ( -0.7071067811865486830, 0.7071067811865464625, 0.000000000000000000 ) ) ;
#119983=ORIENTED_EDGE ( 'NONE', *, *, #142324, .F. ) ;
#119984=LINE ( 'NONE', #11220, #56250 ) ;
#119985=CARTESIAN_POINT ( 'NONE',  ( 24.77004279457776548, 21.73644205237997795, 5.000000000000000000 ) ) ;
#119987=VECTOR ( 'NONE', #110329, 1000.000000000000000 ) ;
#119989=ADVANCED_FACE ( 'NONE', ( #139066 ), #83251, .F. ) ;
#119990=CARTESIAN_POINT ( 'NONE',  ( -11.99451991528749417, 28.92564299267946382, 4.000000000000000000 ) ) ;
#119991=VERTEX_POINT ( 'NONE', #127458 ) ;
#119992=AXIS2_PLACEMENT_3D ( 'NONE', #26588, #60692, #61408 ) ;
#119993=EDGE_CURVE ( 'NONE', #27017, #56485, #72418, .T. ) ;
#119996=DIRECTION ( 'NONE',  ( -0.7071067811865486830, 0.7071067811865464625, 0.000000000000000000 ) ) ;
#119998=ORIENTED_EDGE ( 'NONE', *, *, #84024, .T. ) ;
#120000=AXIS2_PLACEMENT_3D ( 'NONE', #62590, #61208, #140153 ) ;
#120001=PLANE ( 'NONE',  #69747 ) ;
#120005=CARTESIAN_POINT ( 'NONE',  ( -39.18398860626899705, 28.73617430169814568, 5.000000000000000000 ) ) ;
#120006=PLANE ( 'NONE',  #40632 ) ;
#120007=VERTEX_POINT ( 'NONE', #43859 ) ;
#120008=DIRECTION ( 'NONE',  ( -0.7071067811865487940, 0.7071067811865463515, 0.000000000000000000 ) ) ;
#120009=DIRECTION ( 'NONE',  ( -0.000000000000000000, 0.3543493200069153248, 0.9351131265310292928 ) ) ;
#120010=DIRECTION ( 'NONE',  ( 0.6830127018922181881, 0.6830127018922202975, -0.2588190451025214056 ) ) ;
#120012=VERTEX_POINT ( 'NONE', #104988 ) ;
#120013=ORIENTED_EDGE ( 'NONE', *, *, #137652, .T. ) ;
#120015=ORIENTED_EDGE ( 'NONE', *, *, #9525, .T. ) ;
#120016=PLANE ( 'NONE',  #84617 ) ;
#120017=CARTESIAN_POINT ( 'NONE',  ( -17.84387692260746405, -22.22499999999999787, 4.000000000000000000 ) ) ;
#120018=DIRECTION ( 'NONE',  ( -0.7071067811865487940, 0.7071067811865463515, -0.000000000000000000 ) ) ;
#120020=EDGE_LOOP ( 'NONE', ( #85314, #43650, #48822, #56030 ) ) ;
#120021=VECTOR ( 'NONE', #40142, 1000.000000000000000 ) ;
#120022=FACE_OUTER_BOUND ( 'NONE', #26377, .T. ) ;
#120023=CARTESIAN_POINT ( 'NONE',  ( -26.67183060077628198, 5.259292476615661016, 4.000000000000000000 ) ) ;
#120024=VERTEX_POINT ( 'NONE', #5657 ) ;
#120025=CARTESIAN_POINT ( 'NONE',  ( 18.70710678118642178, 20.25929247661551358, 5.000000000000000000 ) ) ;
#120026=EDGE_CURVE ( 'NONE', #118799, #10438, #117970, .T. ) ;
#120028=CARTESIAN_POINT ( 'NONE',  ( -38.99451991528749062, 28.92564299267965211, 4.000000000000000000 ) ) ;
#120029=ORIENTED_EDGE ( 'NONE', *, *, #138106, .T. ) ;
#120030=ORIENTED_EDGE ( 'NONE', *, *, #95195, .F. ) ;
#120031=FACE_BOUND ( 'NONE', #27332, .T. ) ;
#120032=DIRECTION ( 'NONE',  ( 0.6830127018922180770, -0.6830127018922204085, -0.2588190451025213501 ) ) ;
#120033=CARTESIAN_POINT ( 'NONE',  ( 13.82816939922343558, 21.75929247661549581, 4.000000000000000000 ) ) ;
#120034=DIRECTION ( 'NONE',  ( 0.3543493200069162685, -0.000000000000000000, -0.9351131265310288487 ) ) ;
#120035=CARTESIAN_POINT ( 'NONE',  ( -30.48921356237309510, -27.52281430457076894, 5.000000000000000000 ) ) ;
#120036=CARTESIAN_POINT ( 'NONE',  ( -54.48921356237310221, -27.52281430457093236, 5.000000000000000000 ) ) ;
#120037=ORIENTED_EDGE ( 'NONE', *, *, #133809, .F. ) ;
#120038=ADVANCED_FACE ( 'NONE', ( #49926 ), #17271, .T. ) ;
#120039=ORIENTED_EDGE ( 'NONE', *, *, #89629, .F. ) ;
#120042=ADVANCED_FACE ( 'NONE', ( #17949 ), #139799, .F. ) ;
#120043=ADVANCED_FACE ( 'NONE', ( #14055 ), #11914, .T. ) ;
#120044=VERTEX_POINT ( 'NONE', #56200 ) ;
#120047=ADVANCED_FACE ( 'NONE', ( #67038 ), #78625, .T. ) ;
#120049=CARTESIAN_POINT ( 'NONE',  ( 13.26601651615776767, 1.700382741644379081, 5.000000000000000000 ) ) ;
#120050=ORIENTED_EDGE ( 'NONE', *, *, #94592, .F. ) ;
#120052=FACE_OUTER_BOUND ( 'NONE', #115281, .T. ) ;
#120053=EDGE_CURVE ( 'NONE', #17152, #65419, #77916, .T. ) ;
#120054=LINE ( 'NONE', #9897, #41211 ) ;
#120056=VECTOR ( 'NONE', #63441, 1000.000000000000000 ) ;
#120058=CARTESIAN_POINT ( 'NONE',  ( 1.499999999999990896, -8.947814304570737676, 5.000000000000000000 ) ) ;
#120059=VECTOR ( 'NONE', #72532, 999.9999999999998863 ) ;
#120060=VERTEX_POINT ( 'NONE', #111978 ) ;
#120061=FACE_OUTER_BOUND ( 'NONE', #91157, .T. ) ;
#120062=LINE ( 'NONE', #106335, #60513 ) ;
#120065=ORIENTED_EDGE ( 'NONE', *, *, #49724, .T. ) ;
#120066=ORIENTED_EDGE ( 'NONE', *, *, #133756, .T. ) ;
#120067=EDGE_CURVE ( 'NONE', #88880, #17476, #137235, .T. ) ;
#120068=VERTEX_POINT ( 'NONE', #75824 ) ;
#120070=AXIS2_PLACEMENT_3D ( 'NONE', #109248, #8463, #41138 ) ;
#120071=ORIENTED_EDGE ( 'NONE', *, *, #115097, .T. ) ;
#120072=VECTOR ( 'NONE', #129242, 1000.000000000000227 ) ;
#120073=EDGE_CURVE ( 'NONE', #66020, #32821, #62817, .T. ) ;
#120074=PLANE ( 'NONE',  #21189 ) ;
#120077=CARTESIAN_POINT ( 'NONE',  ( 32.99451991528749062, 28.92564299267960948, 4.000000000000000000 ) ) ;
#120078=DIRECTION ( 'NONE',  ( -0.7071067811865486830, -0.7071067811865464625, -0.000000000000000000 ) ) ;
#120079=ORIENTED_EDGE ( 'NONE', *, *, #91387, .T. ) ;
#120080=LINE ( 'NONE', #76646, #60319 ) ;
#120082=VECTOR ( 'NONE', #96632, 1000.000000000000000 ) ;
#120083=DIRECTION ( 'NONE',  ( 0.7071067811865487940, 0.7071067811865463515, 0.000000000000000000 ) ) ;
#120085=PLANE ( 'NONE',  #47543 ) ;
#120087=AXIS2_PLACEMENT_3D ( 'NONE', #141797, #119292, #42494 ) ;
#120089=EDGE_LOOP ( 'NONE', ( #29997, #48157, #21899, #100646 ) ) ;
#120090=EDGE_LOOP ( 'NONE', ( #62643, #131020, #66049, #65393 ) ) ;
#120091=ORIENTED_EDGE ( 'NONE', *, *, #72519, .F. ) ;
#120092=EDGE_CURVE ( 'NONE', #78816, #42201, #64952, .T. ) ;
#120094=VECTOR ( 'NONE', #131974, 1000.000000000000000 ) ;
#120095=ORIENTED_EDGE ( 'NONE', *, *, #72074, .T. ) ;
#120096=VECTOR ( 'NONE', #95259, 1000.000000000000000 ) ;
#120097=VECTOR ( 'NONE', #113565, 1000.000000000000000 ) ;
#120098=LINE ( 'NONE', #20811, #2863 ) ;
#120099=VECTOR ( 'NONE', #27257, 1000.000000000000000 ) ;
#120100=LINE ( 'NONE', #96918, #25492 ) ;
#120101=VERTEX_POINT ( 'NONE', #41040 ) ;
#120102=CARTESIAN_POINT ( 'NONE',  ( -14.67183060077637080, -6.740707523384212863, 4.000000000000000000 ) ) ;
#120103=ORIENTED_EDGE ( 'NONE', *, *, #135070, .F. ) ;
#120104=VECTOR ( 'NONE', #36223, 1000.000000000000000 ) ;
#120105=VECTOR ( 'NONE', #70079, 1000.000000000000227 ) ;
#120109=LINE ( 'NONE', #88244, #106201 ) ;
#120110=LINE ( 'NONE', #52047, #88334 ) ;
#120111=ORIENTED_EDGE ( 'NONE', *, *, #90832, .T. ) ;
#120112=ORIENTED_EDGE ( 'NONE', *, *, #14516, .F. ) ;
#120113=ADVANCED_FACE ( 'NONE', ( #63545 ), #1077, .F. ) ;
#120116=CARTESIAN_POINT ( 'NONE',  ( 17.99451991528748351, 28.92564299267950645, 4.000000000000000000 ) ) ;
#120117=PLANE ( 'NONE',  #54332 ) ;
#120118=CARTESIAN_POINT ( 'NONE',  ( -1.828169399223514624, 9.759292476615625489, 4.000000000000000000 ) ) ;
#120119=LINE ( 'NONE', #7807, #87361 ) ;
#120120=PLANE ( 'NONE',  #83314 ) ;
#120122=EDGE_CURVE ( 'NONE', #108649, #105081, #66377, .T. ) ;
#120123=CARTESIAN_POINT ( 'NONE',  ( 0.000000000000000000, 0.000000000000000000, 5.000000000000000000 ) ) ;
#120124=DIRECTION ( 'NONE',  ( -0.000000000000000000, -0.3543493200069152693, 0.9351131265310292928 ) ) ;
#120126=CARTESIAN_POINT ( 'NONE',  ( 0.000000000000000000, 0.000000000000000000, 5.000000000000000000 ) ) ;
#120127=EDGE_LOOP ( 'NONE', ( #36051, #138365, #1328, #121852 ) ) ;
#120128=LINE ( 'NONE', #20841, #26795 ) ;
#120129=ORIENTED_EDGE ( 'NONE', *, *, #130494, .F. ) ;
#120130=DIRECTION ( 'NONE',  ( 1.000000000000000000, 0.000000000000000000, 0.000000000000000000 ) ) ;
#120133=ADVANCED_FACE ( 'NONE', ( #10529 ), #77274, .F. ) ;
#120134=LINE ( 'NONE', #91819, #6921 ) ;
#120135=ADVANCED_FACE ( 'NONE', ( #43908 ), #122147, .F. ) ;
#120136=ORIENTED_EDGE ( 'NONE', *, *, #77243, .T. ) ;
#120137=CARTESIAN_POINT ( 'NONE',  ( 15.43680103220819788, -12.74070752338415602, 9.898150129686337451 ) ) ;
#120138=EDGE_LOOP ( 'NONE', ( #107422, #70350, #3827, #14095 ) ) ;
#120139=CARTESIAN_POINT ( 'NONE',  ( 11.20666063542144286, 21.75929247661549937, 4.998822639870701856 ) ) ;
#120140=ORIENTED_EDGE ( 'NONE', *, *, #78552, .F. ) ;
#120143=CARTESIAN_POINT ( 'NONE',  ( 5.999999999999956479, 7.007997736742450634, -8.085015511992098780 ) ) ;
#120144=LINE ( 'NONE', #41927, #131953 ) ;
#120145=CARTESIAN_POINT ( 'NONE',  ( 7.828169399223476432, -5.240707523384225297, 4.000000000000000000 ) ) ;
#120147=CARTESIAN_POINT ( 'NONE',  ( 22.49999999999984723, 9.052185695429077583, 5.000000000000000000 ) ) ;
#120151=DIRECTION ( 'NONE',  ( 0.7071067811865487940, 0.7071067811865463515, 0.000000000000000000 ) ) ;
#120153=VERTEX_POINT ( 'NONE', #45361 ) ;
#120154=CARTESIAN_POINT ( 'NONE',  ( 34.42499999999998295, 22.22500000000000142, 5.000000000000000000 ) ) ;
#120155=VERTEX_POINT ( 'NONE', #57654 ) ;
#120157=EDGE_CURVE ( 'NONE', #114421, #18107, #111269, .T. ) ;
#120159=CARTESIAN_POINT ( 'NONE',  ( -4.499999999999962697, -11.94781430457070215, 5.000000000000000000 ) ) ;
#120161=ORIENTED_EDGE ( 'NONE', *, *, #118394, .F. ) ;
#120162=VECTOR ( 'NONE', #2573, 1000.000000000000000 ) ;
#120163=VECTOR ( 'NONE', #3926, 1000.000000000000000 ) ;
#120164=DIRECTION ( 'NONE',  ( -1.000000000000000000, -4.431987436529789959E-15, 0.000000000000000000 ) ) ;
#120165=DIRECTION ( 'NONE',  ( -0.7071067811865487940, 0.7071067811865463515, -0.000000000000000000 ) ) ;
#120166=VECTOR ( 'NONE', #70747, 1000.000000000000000 ) ;
#120167=FACE_OUTER_BOUND ( 'NONE', #74133, .T. ) ;
#120169=EDGE_CURVE ( 'NONE', #94938, #30286, #99687, .T. ) ;
#120170=CARTESIAN_POINT ( 'NONE',  ( -5.510786437626906675, -27.52281430457051314, 5.000000000000000000 ) ) ;
#120171=CARTESIAN_POINT ( 'NONE',  ( -1.499999999999984013, -1.533600742197719580, 5.000000000000000000 ) ) ;
#120172=EDGE_LOOP ( 'NONE', ( #70066, #58372, #89537, #40227 ) ) ;
#120173=DIRECTION ( 'NONE',  ( -0.7071067811865487940, 0.7071067811865463515, 0.000000000000000000 ) ) ;
#120176=LINE ( 'NONE', #66564, #66441 ) ;
#120177=AXIS2_PLACEMENT_3D ( 'NONE', #79208, #12464, #100905 ) ;
#120179=VERTEX_POINT ( 'NONE', #11962 ) ;
#120180=ORIENTED_EDGE ( 'NONE', *, *, #25324, .F. ) ;
#120181=EDGE_LOOP ( 'NONE', ( #111753, #25967, #18543, #36892 ) ) ;
#120184=CARTESIAN_POINT ( 'NONE',  ( 20.67183060077632817, -12.74070752338414891, 4.000000000000000000 ) ) ;
#120185=AXIS2_PLACEMENT_3D ( 'NONE', #101998, #2661, #80971 ) ;
#120186=VECTOR ( 'NONE', #98112, 1000.000000000000227 ) ;
#120187=CARTESIAN_POINT ( 'NONE',  ( -8.510786437626906675, -27.52281430457049183, 5.000000000000000000 ) ) ;
#120188=EDGE_LOOP ( 'NONE', ( #11072, #18561, #21851, #22199 ) ) ;
#120189=EDGE_CURVE ( 'NONE', #8580, #41095, #112023, .T. ) ;
#120190=CARTESIAN_POINT ( 'NONE',  ( -45.29974487139158867, -27.71228299555237840, 4.000000000000000000 ) ) ;
#120192=VECTOR ( 'NONE', #66903, 1000.000000000000000 ) ;
#120194=ORIENTED_EDGE ( 'NONE', *, *, #51149, .F. ) ;
#120195=CARTESIAN_POINT ( 'NONE',  ( -30.18398860626900060, 28.73617430169808173, 5.000000000000000000 ) ) ;
#120197=VECTOR ( 'NONE', #40733, 999.9999999999998863 ) ;
#120198=VECTOR ( 'NONE', #96095, 1000.000000000000000 ) ;
#120199=VECTOR ( 'NONE', #142477, 1000.000000000000000 ) ;
#120200=ORIENTED_EDGE ( 'NONE', *, *, #32491, .T. ) ;
#120203=DIRECTION ( 'NONE',  ( 0.6830127018922181881, 0.6830127018922202975, -0.2588190451025214056 ) ) ;
#120204=DIRECTION ( 'NONE',  ( -0.7071067811865486830, -0.7071067811865464625, 0.000000000000000000 ) ) ;
#120205=DIRECTION ( 'NONE',  ( 0.7071067811865486830, -0.7071067811865464625, -0.000000000000000000 ) ) ;
#120209=CARTESIAN_POINT ( 'NONE',  ( 31.49999999999977973, -8.568876922607721269, 4.000000000000000000 ) ) ;
#120210=ADVANCED_FACE ( 'NONE', ( #98968 ), #143206, .F. ) ;
#120213=EDGE_CURVE ( 'NONE', #6381, #11206, #1765, .T. ) ;
#120214=CARTESIAN_POINT ( 'NONE',  ( 17.02886364525924989, -2.441401769420105339, 4.000000000000000000 ) ) ;
#120215=ORIENTED_EDGE ( 'NONE', *, *, #42010, .F. ) ;
#120216=ORIENTED_EDGE ( 'NONE', *, *, #92274, .F. ) ;
#120217=VECTOR ( 'NONE', #85025, 1000.000000000000000 ) ;
#120218=ADVANCED_FACE ( 'NONE', ( #78671 ), #122880, .F. ) ;
#120220=LINE ( 'NONE', #20932, #14980 ) ;
#120222=LINE ( 'NONE', #20934, #36681 ) ;
#120223=PLANE ( 'NONE',  #15418 ) ;
#120224=CARTESIAN_POINT ( 'NONE',  ( -34.49999999999975131, 10.08746187583914100, 4.000000000000000000 ) ) ;
#120226=EDGE_CURVE ( 'NONE', #14544, #136867, #44657, .T. ) ;
#120227=ORIENTED_EDGE ( 'NONE', *, *, #43535, .F. ) ;
#120229=ORIENTED_EDGE ( 'NONE', *, *, #51129, .F. ) ;
#120230=CARTESIAN_POINT ( 'NONE',  ( -3.328169399223510627, 20.25929247661551003, 4.000000000000000000 ) ) ;
#120231=EDGE_CURVE ( 'NONE', #90674, #136749, #56248, .T. ) ;
#120233=FACE_OUTER_BOUND ( 'NONE', #3120, .T. ) ;
#120234=ORIENTED_EDGE ( 'NONE', *, *, #96680, .F. ) ;
#120235=EDGE_LOOP ( 'NONE', ( #21362, #41752, #57392, #70763 ) ) ;
#120236=EDGE_LOOP ( 'NONE', ( #14010, #76959, #57624, #28696 ) ) ;
#120237=ADVANCED_FACE ( 'NONE', ( #22812 ), #21435, .F. ) ;
#120238=FACE_OUTER_BOUND ( 'NONE', #117756, .T. ) ;
#120239=CARTESIAN_POINT ( 'NONE',  ( 30.48921356237309510, -27.52281430457076894, 5.000000000000000000 ) ) ;
#120241=PLANE ( 'NONE',  #28674 ) ;
#120243=LINE ( 'NONE', #66636, #77476 ) ;
#120244=CARTESIAN_POINT ( 'NONE',  ( -8.292893218813398803, -0.7407075233842735917, 5.000000000000000000 ) ) ;
#120245=DIRECTION ( 'NONE',  ( 0.7071067811865486830, -0.7071067811865464625, -0.000000000000000000 ) ) ;
#120246=EDGE_CURVE ( 'NONE', #80065, #96370, #29795, .T. ) ;
#120247=CARTESIAN_POINT ( 'NONE',  ( 25.49999999999982592, -19.91253812416055169, 4.000000000000000000 ) ) ;
#120248=DIRECTION ( 'NONE',  ( -0.7071067811865486830, -0.7071067811865464625, 0.000000000000000000 ) ) ;
#120249=CARTESIAN_POINT ( 'NONE',  ( 28.49999999999980105, 0.4311230773921797543, 4.000000000000000000 ) ) ;
#120250=DIRECTION ( 'NONE',  ( 0.3543493200069162685, -0.000000000000000000, -0.9351131265310288487 ) ) ;
#120251=VERTEX_POINT ( 'NONE', #135219 ) ;
#120252=EDGE_LOOP ( 'NONE', ( #44592, #126540, #81656, #116651 ) ) ;
#120253=EDGE_CURVE ( 'NONE', #15048, #118228, #36576, .T. ) ;
#120254=EDGE_LOOP ( 'NONE', ( #49312, #57120, #15514, #136002 ) ) ;
#120255=LINE ( 'NONE', #32600, #98104 ) ;
#120257=VECTOR ( 'NONE', #46929, 1000.000000000000227 ) ;
#120259=VECTOR ( 'NONE', #142276, 999.9999999999998863 ) ;
#120260=( BOUNDED_CURVE ( )  B_SPLINE_CURVE ( 3, ( #12183, #76768, #33280, #65175 ),
 .UNSPECIFIED., .F., .T. ) 
 B_SPLINE_CURVE_WITH_KNOTS ( ( 4, 4 ),
 ( 2.779374508378134045, 4.199602562396851368 ),
 .UNSPECIFIED. ) 
 CURVE ( )  GEOMETRIC_REPRESENTATION_ITEM ( )  RATIONAL_B_SPLINE_CURVE ( ( 1.000000000000000000, 0.8388583629366599403, 0.8388583629366599403, 1.000000000000000000 ) ) 
 REPRESENTATION_ITEM ( '' )  );
#120261=VECTOR ( 'NONE', #46716, 1000.000000000000000 ) ;
#120262=EDGE_LOOP ( 'NONE', ( #122537, #107985, #66266, #77310 ) ) ;
#120263=DIRECTION ( 'NONE',  ( -0.3543493200069163240, 0.000000000000000000, 0.9351131265310288487 ) ) ;
#120265=LINE ( 'NONE', #77549, #67222 ) ;
#120267=ORIENTED_EDGE ( 'NONE', *, *, #15388, .F. ) ;
#120268=EDGE_CURVE ( 'NONE', #90585, #11670, #90992, .T. ) ;
#120269=CARTESIAN_POINT ( 'NONE',  ( -11.51078643762690490, -27.52281430457047406, 5.000000000000000000 ) ) ;
#120270=VECTOR ( 'NONE', #84026, 1000.000000000000227 ) ;
#120272=EDGE_CURVE ( 'NONE', #40388, #100787, #135899, .T. ) ;
#120273=CARTESIAN_POINT ( 'NONE',  ( -4.499999999999976019, 3.073033219394619930, -6.593910359670981158 ) ) ;
#120275=VECTOR ( 'NONE', #115471, 1000.000000000000000 ) ;
#120276=VERTEX_POINT ( 'NONE', #59099 ) ;
#120279=CARTESIAN_POINT ( 'NONE',  ( 14.99999999999990230, -4.447814304570775867, 5.000000000000000000 ) ) ;
#120280=EDGE_LOOP ( 'NONE', ( #135865, #30012, #118315, #1157 ) ) ;
#120281=CARTESIAN_POINT ( 'NONE',  ( 4.171830600776443632, -11.24070752338417378, 4.000000000000000000 ) ) ;
#120282=ORIENTED_EDGE ( 'NONE', *, *, #27974, .T. ) ;
#120283=ORIENTED_EDGE ( 'NONE', *, *, #89615, .F. ) ;
#120284=AXIS2_PLACEMENT_3D ( 'NONE', #126951, #39264, #17484 ) ;
#120285=DIRECTION ( 'NONE',  ( 0.7071067811865486830, -0.7071067811865464625, -0.000000000000000000 ) ) ;
#120286=VECTOR ( 'NONE', #19460, 1000.000000000000000 ) ;
#120287=CARTESIAN_POINT ( 'NONE',  ( 18.18398860626898994, 28.73617430169800002, 5.000000000000000000 ) ) ;
#120288=CARTESIAN_POINT ( 'NONE',  ( 36.18398860626899705, 28.73617430169812437, 5.000000000000000000 ) ) ;
#120289=ORIENTED_EDGE ( 'NONE', *, *, #75041, .F. ) ;
#120290=DIRECTION ( 'NONE',  ( 0.3543493200069162685, -0.000000000000000000, -0.9351131265310288487 ) ) ;
#120291=AXIS2_PLACEMENT_3D ( 'NONE', #81742, #67273, #56438 ) ;
#120292=CARTESIAN_POINT ( 'NONE',  ( 20.20710678118640757, 15.75929247661555443, 5.000000000000000000 ) ) ;
#120293=CARTESIAN_POINT ( 'NONE',  ( 33.70701326429281153, -21.74070752338406365, 4.999753212805220670 ) ) ;
#120294=EDGE_LOOP ( 'NONE', ( #9040, #7303, #46590, #67235, #14761 ) ) ;
#120295=CARTESIAN_POINT ( 'NONE',  ( -40.64175702458835815, 15.75929247661555088, 19.34181609438708804 ) ) ;
#120296=VECTOR ( 'NONE', #22831, 999.9999999999998863 ) ;
#120297=CARTESIAN_POINT ( 'NONE',  ( -66.48921356237309510, -27.52281430457101763, 5.000000000000000000 ) ) ;
#120298=VECTOR ( 'NONE', #103085, 1000.000000000000000 ) ;
#120299=ORIENTED_EDGE ( 'NONE', *, *, #59737, .F. ) ;
#120301=CARTESIAN_POINT ( 'NONE',  ( 19.04515773336654050, -21.74070752338406365, 21.72585301388589230 ) ) ;
#120302=ORIENTED_EDGE ( 'NONE', *, *, #136821, .T. ) ;
#120303=VERTEX_POINT ( 'NONE', #69976 ) ;
#120304=VECTOR ( 'NONE', #121869, 1000.000000000000000 ) ;
#120305=DIRECTION ( 'NONE',  ( -0.7071067811865486830, 0.7071067811865464625, 0.000000000000000000 ) ) ;
#120308=ORIENTED_EDGE ( 'NONE', *, *, #96037, .T. ) ;
#120310=DIRECTION ( 'NONE',  ( 0.3543493200069163240, -0.000000000000000000, 0.9351131265310288487 ) ) ;
#120312=LINE ( 'NONE', #8682, #46185 ) ;
#120314=DIRECTION ( 'NONE',  ( -0.6830127018922180770, -0.6830127018922204085, -0.2588190451025213501 ) ) ;
#120315=CARTESIAN_POINT ( 'NONE',  ( -1.499999999999987566, 10.08746187583914633, 4.000000000000000000 ) ) ;
#120317=CARTESIAN_POINT ( 'NONE',  ( -26.21837311707487572, 21.74787736706806740, 4.999607392498048419 ) ) ;
#120318=VECTOR ( 'NONE', #56923, 1000.000000000000227 ) ;
#120319=CARTESIAN_POINT ( 'NONE',  ( -35.99451991528749772, 28.92564299267963079, 4.000000000000000000 ) ) ;
#120320=CARTESIAN_POINT ( 'NONE',  ( 11.81601139373100651, 28.73617430169779041, 5.000000000000000000 ) ) ;
#120321=CARTESIAN_POINT ( 'NONE',  ( -34.42500000000001137, 7.541399257801932876, 5.000000000000000000 ) ) ;
#120323=ORIENTED_EDGE ( 'NONE', *, *, #110697, .F. ) ;
#120324=VERTEX_POINT ( 'NONE', #126434 ) ;
#120325=ORIENTED_EDGE ( 'NONE', *, *, #78541, .F. ) ;
#120327=ORIENTED_EDGE ( 'NONE', *, *, #25642, .F. ) ;
#120328=EDGE_LOOP ( 'NONE', ( #1201, #82019, #98906, #42575 ) ) ;
#120329=ORIENTED_EDGE ( 'NONE', *, *, #137560, .F. ) ;
#120330=CARTESIAN_POINT ( 'NONE',  ( 20.48831394071555678, 6.759292476615645917, 16.35960578974464852 ) ) ;
#120333=ORIENTED_EDGE ( 'NONE', *, *, #101279, .F. ) ;
#120334=CARTESIAN_POINT ( 'NONE',  ( 11.51078643762690490, -27.52281430457047406, 5.000000000000000000 ) ) ;
#120335=CARTESIAN_POINT ( 'NONE',  ( 62.99451991528749772, 28.92564299267982264, 4.000000000000000000 ) ) ;
#120336=FACE_OUTER_BOUND ( 'NONE', #1840, .T. ) ;
#120339=ORIENTED_EDGE ( 'NONE', *, *, #141871, .T. ) ;
#120340=CARTESIAN_POINT ( 'NONE',  ( 13.10362284818588741, 2.655808543615126638, 5.000000000000000000 ) ) ;
#120341=EDGE_CURVE ( 'NONE', #14857, #70673, #137341, .T. ) ;
#120342=FACE_OUTER_BOUND ( 'NONE', #79222, .T. ) ;
#120343=LINE ( 'NONE', #98624, #30817 ) ;
#120344=CARTESIAN_POINT ( 'NONE',  ( 24.25645252394784990, 6.095695649681008632, 4.664440252871067116 ) ) ;
#120345=LINE ( 'NONE', #728, #56157 ) ;
#120346=DIRECTION ( 'NONE',  ( -0.7071067811865486830, -0.7071067811865464625, -0.000000000000000000 ) ) ;
#120348=CARTESIAN_POINT ( 'NONE',  ( 29.99999999999979750, -4.068876922607768343, 4.000000000000000000 ) ) ;
#120350=ORIENTED_EDGE ( 'NONE', *, *, #10728, .F. ) ;
#120353=EDGE_CURVE ( 'NONE', #77093, #9940, #125016, .T. ) ;
#120356=DIRECTION ( 'NONE',  ( -0.6830127018922181881, 0.6830127018922202975, -0.2588190451025214056 ) ) ;
#120357=EDGE_CURVE ( 'NONE', #85580, #54158, #80126, .T. ) ;
#120359=VECTOR ( 'NONE', #44017, 1000.000000000000000 ) ;
#120361=ORIENTED_EDGE ( 'NONE', *, *, #106867, .F. ) ;
#120362=ORIENTED_EDGE ( 'NONE', *, *, #45808, .F. ) ;
#120363=DIRECTION ( 'NONE',  ( 0.7071067811865487940, 0.7071067811865463515, 0.000000000000000000 ) ) ;
#120365=EDGE_CURVE ( 'NONE', #69243, #98525, #114825, .T. ) ;
#120367=VECTOR ( 'NONE', #68995, 1000.000000000000000 ) ;
#120368=PLANE ( 'NONE',  #96389 ) ;
#120369=VECTOR ( 'NONE', #85683, 999.9999999999998863 ) ;
#120370=ORIENTED_EDGE ( 'NONE', *, *, #95340, .T. ) ;
#120372=ORIENTED_EDGE ( 'NONE', *, *, #50346, .F. ) ;
#120373=DIRECTION ( 'NONE',  ( -0.000000000000000000, -0.3543493200069152693, 0.9351131265310292928 ) ) ;
#120375=PLANE ( 'NONE',  #91862 ) ;
#120376=CARTESIAN_POINT ( 'NONE',  ( 42.18398860626899705, 28.73617430169816700, 5.000000000000000000 ) ) ;
#120379=ORIENTED_EDGE ( 'NONE', *, *, #1875, .F. ) ;
#120380=EDGE_CURVE ( 'NONE', #82699, #39180, #124307, .T. ) ;
#120381=CARTESIAN_POINT ( 'NONE',  ( 47.99451991528749062, 28.92564299267971251, 4.000000000000000000 ) ) ;
#120382=ORIENTED_EDGE ( 'NONE', *, *, #108791, .T. ) ;
#120383=ORIENTED_EDGE ( 'NONE', *, *, #136897, .F. ) ;
#120384=VECTOR ( 'NONE', #99095, 1000.000000000000000 ) ;
#120385=ORIENTED_EDGE ( 'NONE', *, *, #58797, .F. ) ;
#120387=EDGE_CURVE ( 'NONE', #98744, #22050, #37303, .T. ) ;
#120388=AXIS2_PLACEMENT_3D ( 'NONE', #65532, #141637, #121291 ) ;
#120389=PLANE ( 'NONE',  #98407 ) ;
#120390=FACE_OUTER_BOUND ( 'NONE', #76133, .T. ) ;
#120391=ORIENTED_EDGE ( 'NONE', *, *, #92697, .T. ) ;
#120392=CARTESIAN_POINT ( 'NONE',  ( 1.930039745135905704, -0.7407075233842770334, 13.87443053587610464 ) ) ;
#120393=AXIS2_PLACEMENT_3D ( 'NONE', #102565, #114809, #3211 ) ;
#120394=CARTESIAN_POINT ( 'NONE',  ( -27.18398860626900060, 28.73617430169806042, 5.000000000000000000 ) ) ;
#120396=ADVANCED_FACE ( 'NONE', ( #3225 ), #25699, .F. ) ;
#120397=PLANE ( 'NONE',  #99941 ) ;
#120398=FACE_BOUND ( 'NONE', #121800, .T. ) ;
#120399=EDGE_CURVE ( 'NONE', #142744, #84062, #106703, .T. ) ;
#120400=ORIENTED_EDGE ( 'NONE', *, *, #34397, .F. ) ;
#120401=PLANE ( 'NONE',  #10887 ) ;
#120403=EDGE_CURVE ( 'NONE', #49613, #21069, #3905, .T. ) ;
#120404=ORIENTED_EDGE ( 'NONE', *, *, #50001, .T. ) ;
#120405=CARTESIAN_POINT ( 'NONE',  ( 0.000000000000000000, 0.000000000000000000, 5.000000000000000000 ) ) ;
#120407=ORIENTED_EDGE ( 'NONE', *, *, #27776, .F. ) ;
#120409=VERTEX_POINT ( 'NONE', #70679 ) ;
#120411=ORIENTED_EDGE ( 'NONE', *, *, #20789, .T. ) ;
#120412=VECTOR ( 'NONE', #31483, 1000.000000000000000 ) ;
#120414=CARTESIAN_POINT ( 'NONE',  ( -3.183988606268992161, 28.73617430169789699, 5.000000000000000000 ) ) ;
#120415=CARTESIAN_POINT ( 'NONE',  ( -30.70710678118632941, 8.259292476615637923, 5.000000000000000000 ) ) ;
#120416=CARTESIAN_POINT ( 'NONE',  ( -41.99451991528749062, 28.92564299267967343, 4.000000000000000000 ) ) ;
#120418=CARTESIAN_POINT ( 'NONE',  ( 75.18398860626899705, 28.73617430169839793, 5.000000000000000000 ) ) ;
#120419=VECTOR ( 'NONE', #33573, 1000.000000000000000 ) ;
#120421=LINE ( 'NONE', #108127, #54812 ) ;
#120422=DIRECTION ( 'NONE',  ( -0.7071067811865486830, -0.7071067811865464625, -0.000000000000000000 ) ) ;
#120423=DIRECTION ( 'NONE',  ( 0.7071067811865487940, -0.7071067811865463515, 0.000000000000000000 ) ) ;
#120424=CARTESIAN_POINT ( 'NONE',  ( 36.48921356237310221, -27.52281430457080802, 5.000000000000000000 ) ) ;
#120425=LINE ( 'NONE', #94073, #55643 ) ;
#120426=ORIENTED_EDGE ( 'NONE', *, *, #133646, .F. ) ;
#120427=ORIENTED_EDGE ( 'NONE', *, *, #17137, .T. ) ;
#120428=AXIS2_PLACEMENT_3D ( 'NONE', #84153, #106548, #7232 ) ;
#120429=ORIENTED_EDGE ( 'NONE', *, *, #93397, .T. ) ;
#120430=CARTESIAN_POINT ( 'NONE',  ( 2.816011393730999401, 28.73617430169785436, 5.000000000000000000 ) ) ;
#120431=DIRECTION ( 'NONE',  ( 0.7071067811865486830, -0.7071067811865464625, -0.000000000000000000 ) ) ;
#120432=ORIENTED_EDGE ( 'NONE', *, *, #131777, .F. ) ;
#120433=EDGE_LOOP ( 'NONE', ( #96971, #25005, #72204, #84979 ) ) ;
#120434=CARTESIAN_POINT ( 'NONE',  ( -17.99999999999987566, 19.55218569542897100, 5.000000000000000000 ) ) ;
#120435=CARTESIAN_POINT ( 'NONE',  ( 15.66846741159846879, -18.74070752338408852, 20.73178291233844917 ) ) ;
#120436=CARTESIAN_POINT ( 'NONE',  ( 36.48921356237310221, -27.52281430457080802, 5.000000000000000000 ) ) ;
#120437=ORIENTED_EDGE ( 'NONE', *, *, #59547, .F. ) ;
#120438=LINE ( 'NONE', #61848, #25462 ) ;
#120439=VECTOR ( 'NONE', #137490, 1000.000000000000000 ) ;
#120440=AXIS2_PLACEMENT_3D ( 'NONE', #113903, #47284, #126897 ) ;
#120441=EDGE_CURVE ( 'NONE', #76924, #80396, #42853, .T. ) ;
#120442=PLANE ( 'NONE',  #130131 ) ;
#120443=EDGE_CURVE ( 'NONE', #59092, #20535, #32689, .T. ) ;
#120445=CARTESIAN_POINT ( 'NONE',  ( -1.809818324255504818, -18.74070752338408852, 7.910009926591512475 ) ) ;
#120446=VERTEX_POINT ( 'NONE', #86353 ) ;
#120448=LINE ( 'NONE', #110302, #125273 ) ;
#120449=PLANE ( 'NONE',  #116703 ) ;
#120450=CARTESIAN_POINT ( 'NONE',  ( 29.67183060077626067, 5.259292476615669010, 4.000000000000000000 ) ) ;
#120451=ORIENTED_EDGE ( 'NONE', *, *, #80528, .F. ) ;
#120452=CARTESIAN_POINT ( 'NONE',  ( 0.000000000000000000, 0.000000000000000000, 5.000000000000000000 ) ) ;
#120454=CARTESIAN_POINT ( 'NONE',  ( -16.39656807105347625, -14.24070752338413648, 19.24067776001722052 ) ) ;
#120456=CARTESIAN_POINT ( 'NONE',  ( 14.81601139373099585, 28.73617430169776910, 5.000000000000000000 ) ) ;
#120457=CARTESIAN_POINT ( 'NONE',  ( 33.48921356237309510, -27.52281430457078670, 5.000000000000000000 ) ) ;
#120460=VECTOR ( 'NONE', #4628, 999.9999999999998863 ) ;
#120461=DIRECTION ( 'NONE',  ( 1.000000000000000000, -0.000000000000000000, 0.000000000000000000 ) ) ;
#120462=CARTESIAN_POINT ( 'NONE',  ( 9.792893218813393474, -20.24070752338407431, 5.000000000000000000 ) ) ;
#120463=VERTEX_POINT ( 'NONE', #63887 ) ;
#120464=VECTOR ( 'NONE', #139783, 1000.000000000000227 ) ;
#120465=AXIS2_PLACEMENT_3D ( 'NONE', #11367, #65841, #109294 ) ;
#120466=AXIS2_PLACEMENT_3D ( 'NONE', #44787, #34582, #43321 ) ;
#120467=FACE_OUTER_BOUND ( 'NONE', #141204, .T. ) ;
#120469=CARTESIAN_POINT ( 'NONE',  ( 30.18398860626900060, 28.73617430169808173, 5.000000000000000000 ) ) ;
#120470=ORIENTED_EDGE ( 'NONE', *, *, #44476, .T. ) ;
#120472=PLANE ( 'NONE',  #11 ) ;
#120473=ORIENTED_EDGE ( 'NONE', *, *, #51752, .F. ) ;
#120474=ORIENTED_EDGE ( 'NONE', *, *, #73362, .T. ) ;
#120475=CARTESIAN_POINT ( 'NONE',  ( -13.84116387061258457, 6.089959206779446355, 4.000000000000000000 ) ) ;
#120477=CARTESIAN_POINT ( 'NONE',  ( 42.18398860626899705, 28.73617430169816700, 5.000000000000000000 ) ) ;
#120479=CARTESIAN_POINT ( 'NONE',  ( 15.18398860626900237, 28.73617430169797871, 5.000000000000000000 ) ) ;
#120480=DIRECTION ( 'NONE',  ( 0.6830127018922181881, 0.6830127018922202975, -0.2588190451025214056 ) ) ;
#120481=DIRECTION ( 'NONE',  ( -0.000000000000000000, 0.3543493200069153248, 0.9351131265310292928 ) ) ;
#120482=VERTEX_POINT ( 'NONE', #10876 ) ;
#120483=CARTESIAN_POINT ( 'NONE',  ( 0.000000000000000000, 0.000000000000000000, 5.000000000000000000 ) ) ;
#120484=CARTESIAN_POINT ( 'NONE',  ( -2.999999999999981792, -13.97847968911260708, -0.1324546996126860776 ) ) ;
#120486=CARTESIAN_POINT ( 'NONE',  ( 39.48921356237310221, -27.52281430457082934, 5.000000000000000000 ) ) ;
#120487=VECTOR ( 'NONE', #21410, 1000.000000000000000 ) ;
#120489=CARTESIAN_POINT ( 'NONE',  ( 14.51078643762690490, -27.52281430457045275, 5.000000000000000000 ) ) ;
#120490=VECTOR ( 'NONE', #78189, 1000.000000000000000 ) ;
#120491=ORIENTED_EDGE ( 'NONE', *, *, #125546, .F. ) ;
#120492=ORIENTED_EDGE ( 'NONE', *, *, #55950, .F. ) ;
#120494=AXIS2_PLACEMENT_3D ( 'NONE', #30618, #63950, #121159 ) ;
#120495=VERTEX_POINT ( 'NONE', #31256 ) ;
#120497=ORIENTED_EDGE ( 'NONE', *, *, #16654, .F. ) ;
#120498=CARTESIAN_POINT ( 'NONE',  ( 8.292893218813398803, 11.25929247661560595, 5.000000000000000000 ) ) ;
#120499=LINE ( 'NONE', #52418, #113376 ) ;
#120500=VECTOR ( 'NONE', #131592, 1000.000000000000000 ) ;
#120501=EDGE_LOOP ( 'NONE', ( #116446, #66542, #134411, #120955 ) ) ;
#120504=ADVANCED_FACE ( 'NONE', ( #87052 ), #66039, .F. ) ;
#120505=LINE ( 'NONE', #109668, #30112 ) ;
#120506=CARTESIAN_POINT ( 'NONE',  ( -24.96654721599509941, 3.964575861396866685, 4.000000000000000000 ) ) ;
#120507=LINE ( 'NONE', #130740, #96267 ) ;
#120508=EDGE_CURVE ( 'NONE', #111356, #126534, #97165, .T. ) ;
#120509=EDGE_CURVE ( 'NONE', #66944, #99905, #119640, .T. ) ;
#120510=VECTOR ( 'NONE', #126400, 1000.000000000000000 ) ;
#120511=ORIENTED_EDGE ( 'NONE', *, *, #62965, .T. ) ;
#120512=LINE ( 'NONE', #132892, #134428 ) ;
#120514=LINE ( 'NONE', #141605, #95873 ) ;
#120515=CARTESIAN_POINT ( 'NONE',  ( 21.96495920677946856, -2.033836129387410985, 4.000000000000000000 ) ) ;
#120516=CARTESIAN_POINT ( 'NONE',  ( 81.18398860626899705, 28.73617430169844056, 5.000000000000000000 ) ) ;
#120517=FACE_OUTER_BOUND ( 'NONE', #85139, .T. ) ;
#120518=DIRECTION ( 'NONE',  ( 0.7071067811865487940, -0.7071067811865463515, 0.000000000000000000 ) ) ;
#120519=EDGE_CURVE ( 'NONE', #85531, #25852, #23305, .T. ) ;
#120521=EDGE_CURVE ( 'NONE', #36667, #4933, #109512, .T. ) ;
#120522=CARTESIAN_POINT ( 'NONE',  ( 20.46326412755669111, -2.625232532701756494, 4.661243073242808954 ) ) ;
#120523=DIRECTION ( 'NONE',  ( 0.7071067811865487940, 0.7071067811865463515, -0.000000000000000000 ) ) ;
#120524=VECTOR ( 'NONE', #51904, 1000.000000000000000 ) ;
#120525=EDGE_LOOP ( 'NONE', ( #33419, #110100, #116407, #79190 ) ) ;
#120526=ORIENTED_EDGE ( 'NONE', *, *, #3928, .T. ) ;
#120528=CARTESIAN_POINT ( 'NONE',  ( 0.000000000000000000, 0.000000000000000000, 5.000000000000000000 ) ) ;
#120530=CARTESIAN_POINT ( 'NONE',  ( 25.49999999999981526, -14.70932175296475819, -11.46312253303843143 ) ) ;
#120531=LINE ( 'NONE', #909, #83186 ) ;
#120532=VERTEX_POINT ( 'NONE', #55146 ) ;
#120538=ORIENTED_EDGE ( 'NONE', *, *, #104688, .F. ) ;
#120539=ORIENTED_EDGE ( 'NONE', *, *, #77611, .F. ) ;
#120540=VECTOR ( 'NONE', #135327, 1000.000000000000000 ) ;
#120541=FACE_OUTER_BOUND ( 'NONE', #36522, .T. ) ;
#120542=EDGE_CURVE ( 'NONE', #100333, #745, #131996, .T. ) ;
#120543=CARTESIAN_POINT ( 'NONE',  ( 18.18398860626898994, 28.73617430169800002, 5.000000000000000000 ) ) ;
#120544=DIRECTION ( 'NONE',  ( 0.6830127018922181881, 0.6830127018922202975, -0.2588190451025214056 ) ) ;
#120546=EDGE_LOOP ( 'NONE', ( #45638, #89761, #102385, #78520 ) ) ;
#120548=LINE ( 'NONE', #140893, #24369 ) ;
#120549=ORIENTED_EDGE ( 'NONE', *, *, #127960, .T. ) ;
#120551=CARTESIAN_POINT ( 'NONE',  ( 56.99451991528749062, 28.92564299267978001, 4.000000000000000000 ) ) ;
#120554=EDGE_CURVE ( 'NONE', #80329, #118697, #21791, .T. ) ;
#120558=ORIENTED_EDGE ( 'NONE', *, *, #136760, .F. ) ;
#120559=DIRECTION ( 'NONE',  ( 1.000000000000000000, 0.000000000000000000, 0.000000000000000000 ) ) ;
#120562=EDGE_CURVE ( 'NONE', #33358, #33570, #141907, .T. ) ;
#120563=DIRECTION ( 'NONE',  ( 0.7071067811865487940, -0.7071067811865463515, 0.000000000000000000 ) ) ;
#120564=CARTESIAN_POINT ( 'NONE',  ( 0.000000000000000000, 0.000000000000000000, 5.000000000000000000 ) ) ;
#120565=ORIENTED_EDGE ( 'NONE', *, *, #37728, .T. ) ;
#120566=ORIENTED_EDGE ( 'NONE', *, *, #9687, .F. ) ;
#120567=CARTESIAN_POINT ( 'NONE',  ( -22.49999999999984013, 21.05218569542895324, 5.000000000000000000 ) ) ;
#120568=CARTESIAN_POINT ( 'NONE',  ( -27.48921356237309155, -27.52281430457074762, 5.000000000000000000 ) ) ;
#120569=VECTOR ( 'NONE', #129047, 999.9999999999998863 ) ;
#120570=ORIENTED_EDGE ( 'NONE', *, *, #64284, .F. ) ;
#120571=VECTOR ( 'NONE', #5434, 1000.000000000000000 ) ;
#120572=EDGE_CURVE ( 'NONE', #103863, #133102, #30540, .T. ) ;
#120573=VECTOR ( 'NONE', #133290, 1000.000000000000000 ) ;
#120574=VERTEX_POINT ( 'NONE', #22472 ) ;
#120575=CARTESIAN_POINT ( 'NONE',  ( -51.18398860626899705, 28.73617430169823095, 5.000000000000000000 ) ) ;
#120576=ORIENTED_EDGE ( 'NONE', *, *, #101244, .F. ) ;
#120578=PLANE ( 'NONE',  #70149 ) ;
#120579=CARTESIAN_POINT ( 'NONE',  ( -2.816011393730999401, 28.73617430169785436, 5.000000000000000000 ) ) ;
#120580=AXIS2_PLACEMENT_3D ( 'NONE', #52386, #29914, #74154 ) ;
#120581=VECTOR ( 'NONE', #117652, 999.9999999999998863 ) ;
#120583=VECTOR ( 'NONE', #313, 1000.000000000000227 ) ;
#120584=EDGE_CURVE ( 'NONE', #115305, #96751, #52943, .T. ) ;
#120585=VECTOR ( 'NONE', #127823, 1000.000000000000227 ) ;
#120586=LINE ( 'NONE', #21309, #136881 ) ;
#120587=FACE_BOUND ( 'NONE', #50537, .T. ) ;
#120588=LINE ( 'NONE', #54668, #71066 ) ;
#120589=LINE ( 'NONE', #87286, #53559 ) ;
#120590=VECTOR ( 'NONE', #54278, 1000.000000000000000 ) ;
#120593=ORIENTED_EDGE ( 'NONE', *, *, #131759, .F. ) ;
#120594=DIRECTION ( 'NONE',  ( -0.7071067811865487940, 0.7071067811865463515, 0.000000000000000000 ) ) ;
#120596=ORIENTED_EDGE ( 'NONE', *, *, #62718, .T. ) ;
#120597=EDGE_LOOP ( 'NONE', ( #123702, #84987, #122207, #135990 ) ) ;
#120599=EDGE_LOOP ( 'NONE', ( #32231, #27533, #81802, #16712, #124176, #105551 ) ) ;
#120600=AXIS2_PLACEMENT_3D ( 'NONE', #57007, #92428, #37370 ) ;
#120602=PLANE ( 'NONE',  #106851 ) ;
#120604=VERTEX_POINT ( 'NONE', #100075 ) ;
#120605=DIRECTION ( 'NONE',  ( 0.7071067811865486830, -0.7071067811865464625, -0.000000000000000000 ) ) ;
#120606=EDGE_CURVE ( 'NONE', #18405, #14052, #78324, .T. ) ;
#120607=AXIS2_PLACEMENT_3D ( 'NONE', #90869, #125630, #115401 ) ;
#120608=CARTESIAN_POINT ( 'NONE',  ( 26.20710678118636494, 9.759292476615616607, 5.000000000000000000 ) ) ;
#120609=DIRECTION ( 'NONE',  ( -0.000000000000000000, 0.000000000000000000, 1.000000000000000000 ) ) ;
#120610=AXIS2_PLACEMENT_3D ( 'NONE', #125033, #124321, #113430 ) ;
#120611=CARTESIAN_POINT ( 'NONE',  ( 8.994519915287490619, 28.92564299267944250, 4.000000000000000000 ) ) ;
#120612=CARTESIAN_POINT ( 'NONE',  ( -66.48921356237309510, -27.52281430457101763, 5.000000000000000000 ) ) ;
#120613=LINE ( 'NONE', #21334, #102878 ) ;
#120614=VECTOR ( 'NONE', #102831, 1000.000000000000000 ) ;
#120615=CARTESIAN_POINT ( 'NONE',  ( 39.18398860626899705, 28.73617430169814568, 5.000000000000000000 ) ) ;
#120616=DIRECTION ( 'NONE',  ( 0.6830127018922180770, -0.6830127018922204085, -0.2588190451025213501 ) ) ;
#120617=ORIENTED_EDGE ( 'NONE', *, *, #86931, .F. ) ;
#120618=CARTESIAN_POINT ( 'NONE',  ( 13.49999999999991118, 14.14708470758592362, -0.5283514160166871143 ) ) ;
#120619=ORIENTED_EDGE ( 'NONE', *, *, #14225, .F. ) ;
#120621=DIRECTION ( 'NONE',  ( -0.7071067811865487940, 0.7071067811865463515, -0.000000000000000000 ) ) ;
#120622=DIRECTION ( 'NONE',  ( 0.7071067811865486830, -0.7071067811865464625, -0.000000000000000000 ) ) ;
#120623=ORIENTED_EDGE ( 'NONE', *, *, #118506, .T. ) ;
#120624=ORIENTED_EDGE ( 'NONE', *, *, #88681, .T. ) ;
#120628=VERTEX_POINT ( 'NONE', #13738 ) ;
#120630=EDGE_CURVE ( 'NONE', #83015, #94514, #136253, .T. ) ;
#120631=CARTESIAN_POINT ( 'NONE',  ( -19.80981832425539224, -18.74070752338409562, 7.910009926591554219 ) ) ;
#120632=VECTOR ( 'NONE', #124366, 1000.000000000000000 ) ;
#120635=ORIENTED_EDGE ( 'NONE', *, *, #130114, .T. ) ;
#120636=PLANE ( 'NONE',  #117424 ) ;
#120637=ORIENTED_EDGE ( 'NONE', *, *, #130387, .F. ) ;
#120638=DIRECTION ( 'NONE',  ( 0.7071067811865486830, -0.7071067811865464625, -0.000000000000000000 ) ) ;
#120639=VECTOR ( 'NONE', #43918, 1000.000000000000000 ) ;
#120640=CARTESIAN_POINT ( 'NONE',  ( 34.92499999999998295, -8.671992264596198652, 16.70802535927752785 ) ) ;
#120641=CARTESIAN_POINT ( 'NONE',  ( -23.67183060077630330, -6.740707523384212863, 4.000000000000000000 ) ) ;
#120642=ORIENTED_EDGE ( 'NONE', *, *, #58710, .F. ) ;
#120643=VECTOR ( 'NONE', #94481, 1000.000000000000000 ) ;
#120644=ORIENTED_EDGE ( 'NONE', *, *, #111250, .F. ) ;
#120645=LINE ( 'NONE', #64879, #70522 ) ;
#120647=CARTESIAN_POINT ( 'NONE',  ( -24.70701326429287903, -21.74070752338406365, 4.999753212805221558 ) ) ;
#120648=ORIENTED_EDGE ( 'NONE', *, *, #74828, .T. ) ;
#120650=DIRECTION ( 'NONE',  ( -0.3543493200069163240, -0.000000000000000000, -0.9351131265310288487 ) ) ;
#120651=VERTEX_POINT ( 'NONE', #100781 ) ;
#120653=AXIS2_PLACEMENT_3D ( 'NONE', #48922, #27139, #126444 ) ;
#120654=CARTESIAN_POINT ( 'NONE',  ( 3.005480084712505828, 28.92564299267936079, 4.000000000000000000 ) ) ;
#120655=CARTESIAN_POINT ( 'NONE',  ( 0.000000000000000000, 0.000000000000000000, 5.000000000000000000 ) ) ;
#120656=AXIS2_PLACEMENT_3D ( 'NONE', #14605, #58887, #125522 ) ;
#120657=CARTESIAN_POINT ( 'NONE',  ( 2.999999999999981792, -8.151047557385066256, -8.977947279169805839 ) ) ;
#120658=CARTESIAN_POINT ( 'NONE',  ( 13.82816939922343735, -2.240707523384259492, 4.000000000000000000 ) ) ;
#120660=DIRECTION ( 'NONE',  ( 0.6830127018922181881, 0.6830127018922202975, -0.2588190451025214056 ) ) ;
#120662=EDGE_CURVE ( 'NONE', #19849, #57984, #11590, .T. ) ;
#120663=ORIENTED_EDGE ( 'NONE', *, *, #72936, .F. ) ;
#120664=DIRECTION ( 'NONE',  ( -0.7071067811865486830, 0.7071067811865464625, 0.000000000000000000 ) ) ;
#120665=EDGE_LOOP ( 'NONE', ( #93940, #88533, #72865, #5917 ) ) ;
#120666=VECTOR ( 'NONE', #108043, 1000.000000000000000 ) ;
#120667=CARTESIAN_POINT ( 'NONE',  ( 23.99999999999983302, 12.83542986846999234, -1.025386466790425333 ) ) ;
#120668=CARTESIAN_POINT ( 'NONE',  ( -8.816011393731004731, 28.73617430169781173, 5.000000000000000000 ) ) ;
#120669=CARTESIAN_POINT ( 'NONE',  ( -6.489213562373093325, -27.52281430457059841, 5.000000000000000000 ) ) ;
#120670=ORIENTED_EDGE ( 'NONE', *, *, #91305, .T. ) ;
#120671=LINE ( 'NONE', #7627, #50664 ) ;
#120672=LINE ( 'NONE', #40484, #30268 ) ;
#120673=CARTESIAN_POINT ( 'NONE',  ( 0.000000000000000000, 0.000000000000000000, 5.000000000000000000 ) ) ;
#120674=ORIENTED_EDGE ( 'NONE', *, *, #33653, .F. ) ;
#120677=CARTESIAN_POINT ( 'NONE',  ( 17.70025512860841488, -27.71228299555193786, 4.000000000000000000 ) ) ;
#120678=DIRECTION ( 'NONE',  ( -0.000000000000000000, 0.000000000000000000, 1.000000000000000000 ) ) ;
#120679=AXIS2_PLACEMENT_3D ( 'NONE', #60820, #104982, #126720 ) ;
#120680=LINE ( 'NONE', #87374, #80661 ) ;
#120682=( BOUNDED_CURVE ( )  B_SPLINE_CURVE ( 3, ( #75507, #41432, #50196, #105270 ),
 .UNSPECIFIED., .F., .F. ) 
 B_SPLINE_CURVE_WITH_KNOTS ( ( 4, 4 ),
 ( 4.350170835173033268, 4.500739107949267570 ),
 .UNSPECIFIED. ) 
 CURVE ( )  GEOMETRIC_REPRESENTATION_ITEM ( )  RATIONAL_B_SPLINE_CURVE ( ( 1.000000000000000000, 0.9981116584018945304, 0.9981116584018945304, 1.000000000000000000 ) ) 
 REPRESENTATION_ITEM ( '' )  );
#120683=CARTESIAN_POINT ( 'NONE',  ( 20.99999999999985079, -21.84840872380822674, 2.849755605029657080 ) ) ;
#120684=VECTOR ( 'NONE', #114050, 1000.000000000000000 ) ;
#120686=LINE ( 'NONE', #54066, #57768 ) ;
#120688=CARTESIAN_POINT ( 'NONE',  ( 14.99999999999989875, -1.209798855135680418, 4.371887122346866050 ) ) ;
#120689=EDGE_LOOP ( 'NONE', ( #28473, #44332, #15835 ) ) ;
#120690=DIRECTION ( 'NONE',  ( -0.7071067811865486830, -0.7071067811865464625, 0.000000000000000000 ) ) ;
#120691=EDGE_CURVE ( 'NONE', #89804, #15358, #46445, .T. ) ;
#120692=ORIENTED_EDGE ( 'NONE', *, *, #34489, .T. ) ;
#120693=VECTOR ( 'NONE', #132685, 1000.000000000000000 ) ;
#120696=CARTESIAN_POINT ( 'NONE',  ( -50.99451991528749062, 28.92564299267973738, 4.000000000000000000 ) ) ;
#120697=AXIS2_PLACEMENT_3D ( 'NONE', #68909, #47191, #91374 ) ;
#120698=CARTESIAN_POINT ( 'NONE',  ( 33.18398860626899705, 28.73617430169810305, 5.000000000000000000 ) ) ;
#120699=ORIENTED_EDGE ( 'NONE', *, *, #72703, .F. ) ;
#120700=VECTOR ( 'NONE', #14756, 1000.000000000000000 ) ;
#120701=DIRECTION ( 'NONE',  ( 1.000000000000000000, 0.000000000000000000, 0.000000000000000000 ) ) ;
#120702=LINE ( 'NONE', #74384, #35063 ) ;
#120703=FACE_OUTER_BOUND ( 'NONE', #86302, .T. ) ;
#120704=CARTESIAN_POINT ( 'NONE',  ( 17.99999999999987210, -10.06887692260770883, 4.000000000000000000 ) ) ;
#120705=CARTESIAN_POINT ( 'NONE',  ( 12.18398860626900060, 28.73617430169795739, 5.000000000000000000 ) ) ;
#120707=EDGE_CURVE ( 'NONE', #11393, #16533, #134137, .T. ) ;
#120708=ORIENTED_EDGE ( 'NONE', *, *, #123265, .F. ) ;
#120709=ORIENTED_EDGE ( 'NONE', *, *, #92583, .T. ) ;
#120710=DIRECTION ( 'NONE',  ( -0.000000000000000000, 0.3543493200069153248, 0.9351131265310292928 ) ) ;
#120711=DIRECTION ( 'NONE',  ( 0.7071067811865487940, 0.7071067811865463515, -0.000000000000000000 ) ) ;
#120712=VECTOR ( 'NONE', #33079, 1000.000000000000227 ) ;
#120713=FACE_OUTER_BOUND ( 'NONE', #38477, .T. ) ;
#120714=FACE_OUTER_BOUND ( 'NONE', #82887, .T. ) ;
#120715=EDGE_CURVE ( 'NONE', #60685, #64647, #1434, .T. ) ;
#120718=LINE ( 'NONE', #112709, #134304 ) ;
#120719=CARTESIAN_POINT ( 'NONE',  ( -54.18398860626899705, 28.73617430169825226, 5.000000000000000000 ) ) ;
#120720=VERTEX_POINT ( 'NONE', #45021 ) ;
#120723=VECTOR ( 'NONE', #135116, 999.9999999999998863 ) ;
#120725=EDGE_CURVE ( 'NONE', #31625, #21087, #80478, .T. ) ;
#120726=LINE ( 'NONE', #97548, #73896 ) ;
#120727=DIRECTION ( 'NONE',  ( 0.7071067811865487940, 0.7071067811865463515, -0.000000000000000000 ) ) ;
#120728=EDGE_CURVE ( 'NONE', #104374, #927, #133423, .T. ) ;
#120729=ORIENTED_EDGE ( 'NONE', *, *, #125279, .T. ) ;
#120730=AXIS2_PLACEMENT_3D ( 'NONE', #64636, #108818, #76234 ) ;
#120731=LINE ( 'NONE', #119990, #100028 ) ;
#120732=EDGE_CURVE ( 'NONE', #55021, #122835, #123274, .T. ) ;
#120733=ORIENTED_EDGE ( 'NONE', *, *, #69919, .T. ) ;
#120734=VECTOR ( 'NONE', #12182, 1000.000000000000000 ) ;
#120736=VECTOR ( 'NONE', #65042, 1000.000000000000000 ) ;
#120737=DIRECTION ( 'NONE',  ( 0.7071067811865486830, -0.7071067811865464625, -0.000000000000000000 ) ) ;
#120738=VERTEX_POINT ( 'NONE', #3571 ) ;
#120739=VECTOR ( 'NONE', #124645, 999.9999999999998863 ) ;
#120740=CARTESIAN_POINT ( 'NONE',  ( -42.18398860626899705, 28.73617430169816700, 5.000000000000000000 ) ) ;
#120741=CARTESIAN_POINT ( 'NONE',  ( 6.183988606268994381, 28.73617430169791476, 5.000000000000000000 ) ) ;
#120742=EDGE_CURVE ( 'NONE', #142125, #1490, #90636, .T. ) ;
#120743=LINE ( 'NONE', #98982, #72025 ) ;
#120744=DIRECTION ( 'NONE',  ( 0.3543493200069162685, -0.000000000000000000, -0.9351131265310288487 ) ) ;
#120746=DIRECTION ( 'NONE',  ( -0.7071067811865486830, -0.7071067811865463515, 0.000000000000000000 ) ) ;
#120747=ORIENTED_EDGE ( 'NONE', *, *, #43235, .T. ) ;
#120748=DIRECTION ( 'NONE',  ( 0.7071067811865487940, 0.7071067811865463515, -0.000000000000000000 ) ) ;
#120749=DIRECTION ( 'NONE',  ( -0.000000000000000000, 0.3543493200069153248, 0.9351131265310292928 ) ) ;
#120751=EDGE_CURVE ( 'NONE', #26035, #119060, #103605, .T. ) ;
#120752=DIRECTION ( 'NONE',  ( -0.6830127018922180770, -0.6830127018922204085, -0.2588190451025213501 ) ) ;
#120753=ORIENTED_EDGE ( 'NONE', *, *, #17027, .F. ) ;
#120754=ORIENTED_EDGE ( 'NONE', *, *, #58621, .T. ) ;
#120756=ORIENTED_EDGE ( 'NONE', *, *, #71068, .F. ) ;
#120758=LINE ( 'NONE', #118617, #12872 ) ;
#120759=CARTESIAN_POINT ( 'NONE',  ( 0.000000000000000000, 0.000000000000000000, 5.000000000000000000 ) ) ;
#120760=DIRECTION ( 'NONE',  ( -0.7071067811865487940, 0.7071067811865463515, -0.000000000000000000 ) ) ;
#120761=VERTEX_POINT ( 'NONE', #40532 ) ;
#120762=ORIENTED_EDGE ( 'NONE', *, *, #2589, .T. ) ;
#120764=DIRECTION ( 'NONE',  ( -0.7071067811865487940, 0.7071067811865463515, -0.000000000000000000 ) ) ;
#120765=DIRECTION ( 'NONE',  ( 0.7071067811865486830, -0.7071067811865464625, -0.000000000000000000 ) ) ;
#120766=EDGE_CURVE ( 'NONE', #75424, #26817, #126791, .T. ) ;
#120767=ORIENTED_EDGE ( 'NONE', *, *, #55282, .F. ) ;
#120768=CARTESIAN_POINT ( 'NONE',  ( 17.51078643762690845, -27.52281430457043143, 5.000000000000000000 ) ) ;
#120769=ADVANCED_FACE ( 'NONE', ( #60152 ), #62285, .F. ) ;
#120770=LINE ( 'NONE', #63587, #112669 ) ;
#120771=DIRECTION ( 'NONE',  ( 0.7071067811865487940, -0.7071067811865463515, 0.000000000000000000 ) ) ;
#120773=EDGE_CURVE ( 'NONE', #23176, #42427, #106443, .T. ) ;
#120774=ORIENTED_EDGE ( 'NONE', *, *, #59729, .F. ) ;
#120775=FACE_BOUND ( 'NONE', #84166, .T. ) ;
#120776=CARTESIAN_POINT ( 'NONE',  ( -7.998069433178966570, -22.22500000000000142, 4.500000000000000888 ) ) ;
#120778=FACE_OUTER_BOUND ( 'NONE', #91053, .T. ) ;
#120779=VECTOR ( 'NONE', #81557, 1000.000000000000000 ) ;
#120780=LINE ( 'NONE', #10576, #115204 ) ;
#120784=EDGE_LOOP ( 'NONE', ( #116954, #104984, #122819 ) ) ;
#120787=ADVANCED_FACE ( 'NONE', ( #114491 ), #26084, .F. ) ;
#120788=ORIENTED_EDGE ( 'NONE', *, *, #57115, .T. ) ;
#120790=VECTOR ( 'NONE', #110507, 1000.000000000000000 ) ;
#120791=VECTOR ( 'NONE', #73963, 1000.000000000000000 ) ;
#120792=LINE ( 'NONE', #109209, #31638 ) ;
#120793=AXIS2_PLACEMENT_3D ( 'NONE', #74505, #29526, #99057 ) ;
#120794=VECTOR ( 'NONE', #68950, 1000.000000000000227 ) ;
#120795=CARTESIAN_POINT ( 'NONE',  ( 13.43359823057990354, 1.153863645259229909, 4.000000000000000000 ) ) ;
#120798=DIRECTION ( 'NONE',  ( -0.6830127018922181881, 0.6830127018922202975, -0.2588190451025214056 ) ) ;
#120799=EDGE_CURVE ( 'NONE', #86413, #8053, #128254, .T. ) ;
#120801=DIRECTION ( 'NONE',  ( 0.7071067811865486830, -0.7071067811865464625, -0.000000000000000000 ) ) ;
#120802=VECTOR ( 'NONE', #80828, 1000.000000000000000 ) ;
#120803=VECTOR ( 'NONE', #17818, 1000.000000000000000 ) ;
#120806=VERTEX_POINT ( 'NONE', #49286 ) ;
#120807=FACE_OUTER_BOUND ( 'NONE', #99343, .T. ) ;
#120808=LINE ( 'NONE', #55581, #118303 ) ;
#120811=EDGE_LOOP ( 'NONE', ( #92023, #7440, #21135, #24969 ) ) ;
#120812=ORIENTED_EDGE ( 'NONE', *, *, #8731, .T. ) ;
#120814=ORIENTED_EDGE ( 'NONE', *, *, #49627, .T. ) ;
#120816=EDGE_CURVE ( 'NONE', #32877, #142614, #94165, .T. ) ;
#120819=CARTESIAN_POINT ( 'NONE',  ( 42.18398860626899705, 28.73617430169816700, 5.000000000000000000 ) ) ;
#120820=VERTEX_POINT ( 'NONE', #139131 ) ;
#120821=DIRECTION ( 'NONE',  ( 0.6830127018922180770, -0.6830127018922204085, -0.2588190451025213501 ) ) ;
#120823=ADVANCED_FACE ( 'NONE', ( #7125 ), #27477, .F. ) ;
#120824=CARTESIAN_POINT ( 'NONE',  ( 33.48921356237309510, -27.52281430457078670, 5.000000000000000000 ) ) ;
#120826=FACE_OUTER_BOUND ( 'NONE', #112552, .T. ) ;
#120827=EDGE_LOOP ( 'NONE', ( #14073, #62943, #17687, #49720 ) ) ;
#120828=AXIS2_PLACEMENT_3D ( 'NONE', #130804, #19156, #9692 ) ;
#120829=EDGE_CURVE ( 'NONE', #8757, #16774, #82596, .T. ) ;
#120830=CARTESIAN_POINT ( 'NONE',  ( 0.000000000000000000, 0.000000000000000000, 5.000000000000000000 ) ) ;
#120831=ORIENTED_EDGE ( 'NONE', *, *, #54152, .F. ) ;
#120832=VECTOR ( 'NONE', #107278, 1000.000000000000000 ) ;
#120833=EDGE_LOOP ( 'NONE', ( #14517, #107342, #102161, #32730 ) ) ;
#120836=ORIENTED_EDGE ( 'NONE', *, *, #131844, .T. ) ;
#120837=VECTOR ( 'NONE', #134310, 999.9999999999998863 ) ;
#120840=EDGE_CURVE ( 'NONE', #70901, #92286, #49982, .T. ) ;
#120841=EDGE_LOOP ( 'NONE', ( #69674, #130819, #115906, #139637 ) ) ;
#120842=CARTESIAN_POINT ( 'NONE',  ( -34.92500000000001137, 6.759292476615653023, 4.255531930566238685 ) ) ;
#120843=ORIENTED_EDGE ( 'NONE', *, *, #99117, .F. ) ;
#120844=VECTOR ( 'NONE', #61827, 1000.000000000000000 ) ;
#120846=DIRECTION ( 'NONE',  ( -0.6830127018922181881, 0.6830127018922202975, -0.2588190451025214056 ) ) ;
#120847=CARTESIAN_POINT ( 'NONE',  ( -0.7071067811865363595, 20.25929247661552424, 5.000000000000000000 ) ) ;
#120849=CARTESIAN_POINT ( 'NONE',  ( -14.99999999999989164, 16.55218569542900298, 5.000000000000000000 ) ) ;
#120850=EDGE_LOOP ( 'NONE', ( #101646, #92015, #88028, #16974 ) ) ;
#120851=ORIENTED_EDGE ( 'NONE', *, *, #35265, .F. ) ;
#120852=VECTOR ( 'NONE', #102053, 999.9999999999998863 ) ;
#120853=ORIENTED_EDGE ( 'NONE', *, *, #79095, .T. ) ;
#120856=VECTOR ( 'NONE', #116617, 999.9999999999998863 ) ;
#120857=CARTESIAN_POINT ( 'NONE',  ( -34.92500000000001137, -22.22500000000000142, 4.500000000000000888 ) ) ;
#120858=DIRECTION ( 'NONE',  ( -0.6830127018922180770, -0.6830127018922204085, -0.2588190451025213501 ) ) ;
#120859=FACE_OUTER_BOUND ( 'NONE', #25626, .T. ) ;
#120861=LINE ( 'NONE', #44798, #41758 ) ;
#120862=DIRECTION ( 'NONE',  ( 0.7071067811865487940, 0.7071067811865463515, 0.000000000000000000 ) ) ;
#120863=ORIENTED_EDGE ( 'NONE', *, *, #110836, .T. ) ;
#120864=CARTESIAN_POINT ( 'NONE',  ( 15.18398860626900237, 28.73617430169797871, 5.000000000000000000 ) ) ;
#120865=ADVANCED_FACE ( 'NONE', ( #6399 ), #38381, .F. ) ;
#120866=VECTOR ( 'NONE', #63836, 1000.000000000000000 ) ;
#120868=CARTESIAN_POINT ( 'NONE',  ( -21.79614956108759216, 8.475608720613168501, 4.664130618528514738 ) ) ;
#120869=ORIENTED_EDGE ( 'NONE', *, *, #47023, .T. ) ;
#120872=ORIENTED_EDGE ( 'NONE', *, *, #17825, .T. ) ;
#120873=CARTESIAN_POINT ( 'NONE',  ( -45.29974487139158867, -27.71228299555237840, 4.000000000000000000 ) ) ;
#120874=EDGE_CURVE ( 'NONE', #42386, #11025, #37685, .T. ) ;
#120875=EDGE_LOOP ( 'NONE', ( #75079, #142105, #24404 ) ) ;
#120876=CARTESIAN_POINT ( 'NONE',  ( 15.79289321881335084, -14.24070752338414003, 5.000000000000000000 ) ) ;
#120877=VECTOR ( 'NONE', #132710, 1000.000000000000000 ) ;
#120878=ORIENTED_EDGE ( 'NONE', *, *, #140476, .T. ) ;
#120879=DIRECTION ( 'NONE',  ( -0.7071067811865486830, -0.7071067811865464625, 0.000000000000000000 ) ) ;
#120880=EDGE_LOOP ( 'NONE', ( #75752, #93969, #125004, #102108 ) ) ;
#120881=LINE ( 'NONE', #22972, #52220 ) ;
#120883=EDGE_CURVE ( 'NONE', #9195, #91342, #95600, .T. ) ;
#120884=DIRECTION ( 'NONE',  ( 0.7071067811865487940, 0.7071067811865463515, 0.000000000000000000 ) ) ;
#120885=DIRECTION ( 'NONE',  ( -0.7071067811865487940, 0.7071067811865463515, -0.000000000000000000 ) ) ;
#120886=ADVANCED_FACE ( 'NONE', ( #81925 ), #117332, .F. ) ;
#120888=CARTESIAN_POINT ( 'NONE',  ( 13.49999999999991473, 16.46639925780209524, 5.000000000000000000 ) ) ;
#120890=CARTESIAN_POINT ( 'NONE',  ( -62.99451991528749772, 28.92564299267982264, 4.000000000000000000 ) ) ;
#120894=VECTOR ( 'NONE', #67388, 999.9999999999998863 ) ;
#120895=AXIS2_PLACEMENT_3D ( 'NONE', #102257, #13765, #2163 ) ;
#120896=CARTESIAN_POINT ( 'NONE',  ( 14.99999999999990408, 10.55218569542906515, 5.000000000000000000 ) ) ;
#120898=EDGE_CURVE ( 'NONE', #104048, #109338, #4985, .T. ) ;
#120899=ORIENTED_EDGE ( 'NONE', *, *, #53013, .T. ) ;
#120900=ORIENTED_EDGE ( 'NONE', *, *, #132337, .F. ) ;
#120901=AXIS2_PLACEMENT_3D ( 'NONE', #3318, #135996, #93912 ) ;
#120903=DIRECTION ( 'NONE',  ( -0.7071067811865487940, 0.7071067811865463515, -0.000000000000000000 ) ) ;
#120904=ORIENTED_EDGE ( 'NONE', *, *, #116140, .T. ) ;
#120906=CARTESIAN_POINT ( 'NONE',  ( -0.7070132642930445632, -21.74070752338405654, 4.999753212805222446 ) ) ;
#120907=CARTESIAN_POINT ( 'NONE',  ( 0.000000000000000000, 0.000000000000000000, 5.000000000000000000 ) ) ;
#120908=AXIS2_PLACEMENT_3D ( 'NONE', #46644, #35753, #14674 ) ;
#120909=DIRECTION ( 'NONE',  ( -0.000000000000000000, -0.3543493200069152693, 0.9351131265310292928 ) ) ;
#120911=VECTOR ( 'NONE', #65557, 1000.000000000000000 ) ;
#120913=ORIENTED_EDGE ( 'NONE', *, *, #95956, .F. ) ;
#120914=FACE_OUTER_BOUND ( 'NONE', #42937, .T. ) ;
#120918=ADVANCED_FACE ( 'NONE', ( #118034 ), #43380, .T. ) ;
#120919=CARTESIAN_POINT ( 'NONE',  ( 0.7933393645784738712, 21.75929247661549937, 4.998822639870705409 ) ) ;
#120920=DIRECTION ( 'NONE',  ( -0.7071067811865486830, -0.7071067811865464625, 0.000000000000000000 ) ) ;
#120921=CARTESIAN_POINT ( 'NONE',  ( 48.48921356237309510, -27.52281430457089328, 5.000000000000000000 ) ) ;
#120922=ORIENTED_EDGE ( 'NONE', *, *, #71155, .T. ) ;
#120923=CARTESIAN_POINT ( 'NONE',  ( -12.79289321881336683, -20.24070752338407431, 5.000000000000000000 ) ) ;
#120925=LINE ( 'NONE', #129654, #78033 ) ;
#120926=EDGE_CURVE ( 'NONE', #51106, #94631, #20163, .T. ) ;
#120927=DIRECTION ( 'NONE',  ( -0.7071067811865486830, -0.7071067811865464625, 0.000000000000000000 ) ) ;
#120928=VERTEX_POINT ( 'NONE', #63014 ) ;
#120929=ORIENTED_EDGE ( 'NONE', *, *, #32400, .T. ) ;
#120930=VERTEX_POINT ( 'NONE', #107188 ) ;
#120932=EDGE_LOOP ( 'NONE', ( #102299, #78605, #44029, #137311 ) ) ;
#120933=DIRECTION ( 'NONE',  ( 1.000000000000000000, 0.000000000000000000, 0.000000000000000000 ) ) ;
#120936=DIRECTION ( 'NONE',  ( -0.7071067811865486830, 0.7071067811865464625, 0.000000000000000000 ) ) ;
#120937=CARTESIAN_POINT ( 'NONE',  ( 17.29289321881334018, -15.74070752338412049, 5.000000000000000000 ) ) ;
#120938=AXIS2_PLACEMENT_3D ( 'NONE', #82682, #15933, #125472 ) ;
#120940=ORIENTED_EDGE ( 'NONE', *, *, #65388, .F. ) ;
#120941=VECTOR ( 'NONE', #36683, 1000.000000000000000 ) ;
#120942=LINE ( 'NONE', #32527, #104486 ) ;
#120943=EDGE_CURVE ( 'NONE', #93492, #124824, #9264, .T. ) ;
#120944=CARTESIAN_POINT ( 'NONE',  ( -30.70710678118632231, -9.740707523384179112, 5.000000000000000000 ) ) ;
#120945=VECTOR ( 'NONE', #33429, 1000.000000000000227 ) ;
#120946=ORIENTED_EDGE ( 'NONE', *, *, #66807, .F. ) ;
#120947=ORIENTED_EDGE ( 'NONE', *, *, #51236, .T. ) ;
#120948=ORIENTED_EDGE ( 'NONE', *, *, #19469, .F. ) ;
#120949=DIRECTION ( 'NONE',  ( -0.000000000000000000, 0.000000000000000000, 1.000000000000000000 ) ) ;
#120950=CARTESIAN_POINT ( 'NONE',  ( 42.48921356237308800, -27.52281430457085065, 5.000000000000000000 ) ) ;
#120951=PLANE ( 'NONE',  #7144 ) ;
#120952=CARTESIAN_POINT ( 'NONE',  ( 14.99999999999989875, -18.41253812416056590, 4.000000000000000000 ) ) ;
#120953=EDGE_CURVE ( 'NONE', #49295, #114174, #97750, .T. ) ;
#120954=CARTESIAN_POINT ( 'NONE',  ( -48.18398860626899705, 28.73617430169820608, 5.000000000000000000 ) ) ;
#120955=ORIENTED_EDGE ( 'NONE', *, *, #8426, .T. ) ;
#120956=ORIENTED_EDGE ( 'NONE', *, *, #92101, .T. ) ;
#120958=DIRECTION ( 'NONE',  ( 0.3543493200069162685, -0.000000000000000000, -0.9351131265310288487 ) ) ;
#120960=ORIENTED_EDGE ( 'NONE', *, *, #77486, .F. ) ;
#120961=VERTEX_POINT ( 'NONE', #96282 ) ;
#120962=AXIS2_PLACEMENT_3D ( 'NONE', #111311, #134529, #2536 ) ;
#120963=VECTOR ( 'NONE', #142660, 1000.000000000000000 ) ;
#120964=DIRECTION ( 'NONE',  ( 1.000000000000000000, -0.000000000000000000, -0.000000000000000000 ) ) ;
#120966=CARTESIAN_POINT ( 'NONE',  ( -10.49999999999992895, -7.420205493532911589, -2.617629953481277028 ) ) ;
#120968=EDGE_CURVE ( 'NONE', #59821, #66777, #54285, .T. ) ;
#120969=FACE_OUTER_BOUND ( 'NONE', #59364, .T. ) ;
#120970=PLANE ( 'NONE',  #92348 ) ;
#120972=CARTESIAN_POINT ( 'NONE',  ( 16.49999999999988631, -11.94781430457070392, 5.000000000000000000 ) ) ;
#120973=ORIENTED_EDGE ( 'NONE', *, *, #94213, .F. ) ;
#120976=DIRECTION ( 'NONE',  ( 0.6830127018922180770, -0.6830127018922204085, -0.2588190451025213501 ) ) ;
#120979=DIRECTION ( 'NONE',  ( -0.7071067811865487940, 0.7071067811865463515, 0.000000000000000000 ) ) ;
#120980=ORIENTED_EDGE ( 'NONE', *, *, #56784, .T. ) ;
#120981=EDGE_CURVE ( 'NONE', #135031, #24532, #23007, .T. ) ;
#120982=CARTESIAN_POINT ( 'NONE',  ( -6.938893903907228378E-15, -16.02097659208071789, -11.96015758381208727 ) ) ;
#120983=ORIENTED_EDGE ( 'NONE', *, *, #127962, .F. ) ;
#120984=VERTEX_POINT ( 'NONE', #101318 ) ;
#120985=VECTOR ( 'NONE', #14656, 1000.000000000000000 ) ;
#120986=ORIENTED_EDGE ( 'NONE', *, *, #120766, .T. ) ;
#120987=DIRECTION ( 'NONE',  ( -0.6830127018922180770, -0.6830127018922204085, -0.2588190451025213501 ) ) ;
#120988=CARTESIAN_POINT ( 'NONE',  ( 30.79333936457826937, 21.75929247661550647, 4.998822639870708073 ) ) ;
#120989=LINE ( 'NONE', #20236, #137534 ) ;
#120991=CARTESIAN_POINT ( 'NONE',  ( -22.49999999999984723, -9.462702396501025959, -9.474982329943465231 ) ) ;
#120992=CARTESIAN_POINT ( 'NONE',  ( -17.29289321881333663, -18.74070752338409562, 5.000000000000000000 ) ) ;
#120993=CARTESIAN_POINT ( 'NONE',  ( -21.00548008471250938, 28.92564299267923644, 4.000000000000000000 ) ) ;
#120994=VECTOR ( 'NONE', #74163, 1000.000000000000000 ) ;
#120996=CARTESIAN_POINT ( 'NONE',  ( 20.99999999999985079, -18.03360074219755660, 5.000000000000000000 ) ) ;
#120997=EDGE_CURVE ( 'NONE', #14168, #125750, #14305, .T. ) ;
#120998=AXIS2_PLACEMENT_3D ( 'NONE', #45128, #76301, #89999 ) ;
#120999=VECTOR ( 'NONE', #6125, 1000.000000000000000 ) ;
#121000=EDGE_CURVE ( 'NONE', #23978, #119191, #123812, .T. ) ;
#121001=DIRECTION ( 'NONE',  ( 0.6830127018922181881, 0.6830127018922202975, -0.2588190451025214056 ) ) ;
#121002=CARTESIAN_POINT ( 'NONE',  ( 8.510786437626906675, -27.52281430457049183, 5.000000000000000000 ) ) ;
#121003=VERTEX_POINT ( 'NONE', #1953 ) ;
#121004=ORIENTED_EDGE ( 'NONE', *, *, #139482, .T. ) ;
#121006=VECTOR ( 'NONE', #36755, 1000.000000000000000 ) ;
#121008=FACE_OUTER_BOUND ( 'NONE', #142257, .T. ) ;
#121010=ORIENTED_EDGE ( 'NONE', *, *, #839, .T. ) ;
#121013=CARTESIAN_POINT ( 'NONE',  ( -2.999999999999981792, 12.25461709320620507, -10.07315571508697971 ) ) ;
#121015=DIRECTION ( 'NONE',  ( 1.000000000000000000, 0.000000000000000000, 0.000000000000000000 ) ) ;
#121016=EDGE_CURVE ( 'NONE', #81493, #83949, #69428, .T. ) ;
#121017=LINE ( 'NONE', #110824, #53343 ) ;
#121018=EDGE_LOOP ( 'NONE', ( #32004, #26109, #109965, #95265 ) ) ;
#121019=CARTESIAN_POINT ( 'NONE',  ( 12.48921356237309155, -27.52281430457064104, 5.000000000000000000 ) ) ;
#121020=ORIENTED_EDGE ( 'NONE', *, *, #118077, .F. ) ;
#121022=VECTOR ( 'NONE', #123597, 1000.000000000000000 ) ;
#121027=DIRECTION ( 'NONE',  ( 0.6830127018922181881, 0.6830127018922202975, -0.2588190451025214056 ) ) ;
#121028=CARTESIAN_POINT ( 'NONE',  ( -27.41161490594811667, 22.22500000000000142, 4.777194822843815913 ) ) ;
#121029=VERTEX_POINT ( 'NONE', #89726 ) ;
#121030=ORIENTED_EDGE ( 'NONE', *, *, #108121, .T. ) ;
#121031=VERTEX_POINT ( 'NONE', #121624 ) ;
#121032=FACE_OUTER_BOUND ( 'NONE', #113710, .T. ) ;
#121033=CARTESIAN_POINT ( 'NONE',  ( 33.71757738642545377, -21.73023691814492508, 5.000000000000000000 ) ) ;
#121035=LINE ( 'NONE', #21738, #84458 ) ;
#121036=DIRECTION ( 'NONE',  ( 0.7071067811865486830, -0.7071067811865464625, -0.000000000000000000 ) ) ;
#121037=EDGE_CURVE ( 'NONE', #126389, #56485, #57848, .T. ) ;
#121038=ORIENTED_EDGE ( 'NONE', *, *, #44533, .T. ) ;
#121040=DIRECTION ( 'NONE',  ( -0.7071067811865486830, -0.7071067811865464625, 0.000000000000000000 ) ) ;
#121041=VECTOR ( 'NONE', #116232, 1000.000000000000000 ) ;
#121042=CARTESIAN_POINT ( 'NONE',  ( 0.000000000000000000, 0.000000000000000000, 5.000000000000000000 ) ) ;
#121043=ORIENTED_EDGE ( 'NONE', *, *, #22525, .F. ) ;
#121046=CARTESIAN_POINT ( 'NONE',  ( 33.18398860626899705, 28.73617430169810305, 5.000000000000000000 ) ) ;
#121047=ORIENTED_EDGE ( 'NONE', *, *, #30090, .F. ) ;
#121048=LINE ( 'NONE', #87717, #92652 ) ;
#121049=VERTEX_POINT ( 'NONE', #132563 ) ;
#121050=VERTEX_POINT ( 'NONE', #22292 ) ;
#121051=DIRECTION ( 'NONE',  ( -0.000000000000000000, -0.3543493200069152693, 0.9351131265310292928 ) ) ;
#121052=CARTESIAN_POINT ( 'NONE',  ( -4.998069433178984333, -22.22500000000000142, 4.500000000000000888 ) ) ;
#121053=EDGE_LOOP ( 'NONE', ( #16619, #97067, #120426, #21716 ) ) ;
#121054=DIRECTION ( 'NONE',  ( -0.7071067811865486830, 0.7071067811865464625, 0.000000000000000000 ) ) ;
#121055=VECTOR ( 'NONE', #122471, 1000.000000000000000 ) ;
#121056=CARTESIAN_POINT ( 'NONE',  ( -24.29974487139158867, -27.71228299555223273, 4.000000000000000000 ) ) ;
#121057=ADVANCED_FACE ( 'NONE', ( #134692 ), #56444, .T. ) ;
#121058=FACE_OUTER_BOUND ( 'NONE', #96367, .T. ) ;
#121059=CARTESIAN_POINT ( 'NONE',  ( 0.000000000000000000, 0.000000000000000000, 5.000000000000000000 ) ) ;
#121060=EDGE_CURVE ( 'NONE', #87749, #115239, #33256, .T. ) ;
#121061=DIRECTION ( 'NONE',  ( 0.6830127018922180770, -0.6830127018922204085, -0.2588190451025213501 ) ) ;
#121062=DIRECTION ( 'NONE',  ( 0.6830127018922181881, 0.6830127018922202975, -0.2588190451025214056 ) ) ;
#121063=DIRECTION ( 'NONE',  ( -0.000000000000000000, -0.3543493200069152693, 0.9351131265310292928 ) ) ;
#121064=CARTESIAN_POINT ( 'NONE',  ( -4.499999999999968914, 4.466399257802219580, 5.000000000000000000 ) ) ;
#121065=LINE ( 'NONE', #40673, #61885 ) ;
#121066=DIRECTION ( 'NONE',  ( -0.7071067811865486830, 0.7071067811865464625, 0.000000000000000000 ) ) ;
#121068=CARTESIAN_POINT ( 'NONE',  ( -3.183988606268992161, 28.73617430169789699, 5.000000000000000000 ) ) ;
#121069=CARTESIAN_POINT ( 'NONE',  ( -34.49999999999976552, 7.464255608400418573, 4.994342998332163219 ) ) ;
#121070=DIRECTION ( 'NONE',  ( 0.3543493200069162685, -0.000000000000000000, -0.9351131265310288487 ) ) ;
#121071=EDGE_CURVE ( 'NONE', #81589, #74837, #110731, .T. ) ;
#121074=ORIENTED_EDGE ( 'NONE', *, *, #29909, .T. ) ;
#121076=EDGE_LOOP ( 'NONE', ( #134997, #7149, #9785, #133362 ) ) ;
#121077=ORIENTED_EDGE ( 'NONE', *, *, #823, .F. ) ;
#121078=EDGE_LOOP ( 'NONE', ( #74212, #126874, #33956, #5838 ) ) ;
#121079=DIRECTION ( 'NONE',  ( -1.000000000000000000, 0.000000000000000000, -0.000000000000000000 ) ) ;
#121080=FACE_OUTER_BOUND ( 'NONE', #74033, .T. ) ;
#121081=VECTOR ( 'NONE', #26638, 1000.000000000000000 ) ;
#121082=EDGE_LOOP ( 'NONE', ( #139591, #133176, #32302, #141706 ) ) ;
#121083=CARTESIAN_POINT ( 'NONE',  ( 20.81601139373100295, 28.73617430169773002, 5.000000000000000000 ) ) ;
#121084=CARTESIAN_POINT ( 'NONE',  ( 37.98012225071429526, -17.24070752338409918, 20.23474786156478089 ) ) ;
#121085=EDGE_CURVE ( 'NONE', #98086, #133451, #133259, .T. ) ;
#121086=FACE_OUTER_BOUND ( 'NONE', #8922, .T. ) ;
#121087=CARTESIAN_POINT ( 'NONE',  ( 27.48921356237309155, -27.52281430457074762, 5.000000000000000000 ) ) ;
#121088=ORIENTED_EDGE ( 'NONE', *, *, #137200, .T. ) ;
#121089=EDGE_CURVE ( 'NONE', #14142, #96671, #112907, .T. ) ;
#121090=CARTESIAN_POINT ( 'NONE',  ( 8.999999999999937828, -19.06887692260761469, 4.000000000000000000 ) ) ;
#121091=FACE_OUTER_BOUND ( 'NONE', #41888, .T. ) ;
#121093=DIRECTION ( 'NONE',  ( 0.3543493200069162685, -0.000000000000000000, -0.9351131265310288487 ) ) ;
#121094=CARTESIAN_POINT ( 'NONE',  ( 0.000000000000000000, 0.000000000000000000, 5.000000000000000000 ) ) ;
#121097=EDGE_CURVE ( 'NONE', #57727, #89471, #78156, .T. ) ;
#121098=CARTESIAN_POINT ( 'NONE',  ( 29.53839644629411509, -9.740707523384184441, 17.74957260769617662 ) ) ;
#121099=ORIENTED_EDGE ( 'NONE', *, *, #75155, .F. ) ;
#121100=ORIENTED_EDGE ( 'NONE', *, *, #109152, .F. ) ;
#121104=DIRECTION ( 'NONE',  ( -0.7071067811865486830, -0.7071067811865464625, -0.000000000000000000 ) ) ;
#121105=EDGE_CURVE ( 'NONE', #91841, #8931, #133950, .T. ) ;
#121106=AXIS2_PLACEMENT_3D ( 'NONE', #94994, #5115, #49415 ) ;
#121107=PLANE ( 'NONE',  #34144 ) ;
#121109=CARTESIAN_POINT ( 'NONE',  ( 14.26396771883894132, 22.22500000000000142, 23.63953864884001987 ) ) ;
#121112=VERTEX_POINT ( 'NONE', #138235 ) ;
#121113=VERTEX_POINT ( 'NONE', #61434 ) ;
#121114=EDGE_CURVE ( 'NONE', #90422, #52778, #67838, .T. ) ;
#121117=CARTESIAN_POINT ( 'NONE',  ( 28.17183060077627133, 6.759292476615649470, 4.000000000000000000 ) ) ;
#121118=DIRECTION ( 'NONE',  ( 0.3543493200069162685, -0.000000000000000000, -0.9351131265310288487 ) ) ;
#121120=VERTEX_POINT ( 'NONE', #83887 ) ;
#121122=ORIENTED_EDGE ( 'NONE', *, *, #56926, .T. ) ;
#121124=DIRECTION ( 'NONE',  ( 0.7071067811865487940, -0.7071067811865463515, 0.000000000000000000 ) ) ;
#121125=EDGE_CURVE ( 'NONE', #139988, #69350, #105575, .T. ) ;
#121128=CARTESIAN_POINT ( 'NONE',  ( 39.18398860626899705, 28.73617430169814568, 5.000000000000000000 ) ) ;
#121129=ORIENTED_EDGE ( 'NONE', *, *, #113697, .F. ) ;
#121130=VERTEX_POINT ( 'NONE', #115009 ) ;
#121131=ORIENTED_EDGE ( 'NONE', *, *, #133494, .F. ) ;
#121132=AXIS2_PLACEMENT_3D ( 'NONE', #1173, #46911, #68627 ) ;
#121133=CARTESIAN_POINT ( 'NONE',  ( 18.48921356237309510, -27.52281430457068367, 5.000000000000000000 ) ) ;
#121134=CARTESIAN_POINT ( 'NONE',  ( 33.75860074219772855, 21.72500000000000142, 5.000000000000000000 ) ) ;
#121135=EDGE_LOOP ( 'NONE', ( #76424, #19832, #116846, #91275 ) ) ;
#121137=CARTESIAN_POINT ( 'NONE',  ( 10.49999999999993250, 19.46639925780205616, 5.000000000000000000 ) ) ;
#121138=EDGE_CURVE ( 'NONE', #86186, #94959, #38922, .T. ) ;
#121139=LINE ( 'NONE', #10234, #133544 ) ;
#121141=CARTESIAN_POINT ( 'NONE',  ( -18.18398860626898994, 28.73617430169800002, 5.000000000000000000 ) ) ;
#121142=VECTOR ( 'NONE', #102687, 1000.000000000000000 ) ;
#121143=FACE_BOUND ( 'NONE', #118846, .T. ) ;
#121144=ORIENTED_EDGE ( 'NONE', *, *, #106500, .T. ) ;
#121145=FACE_OUTER_BOUND ( 'NONE', #143474, .T. ) ;
#121146=EDGE_CURVE ( 'NONE', #88713, #52625, #106276, .T. ) ;
#121147=DIRECTION ( 'NONE',  ( 0.6830127018922181881, 0.6830127018922202975, -0.2588190451025214056 ) ) ;
#121148=CARTESIAN_POINT ( 'NONE',  ( 32.29289321881323360, -15.74070752338412049, 5.000000000000000000 ) ) ;
#121149=EDGE_LOOP ( 'NONE', ( #1264, #67014, #96908, #127469 ) ) ;
#121150=LINE ( 'NONE', #134195, #59707 ) ;
#121152=ORIENTED_EDGE ( 'NONE', *, *, #103393, .T. ) ;
#121157=VECTOR ( 'NONE', #36694, 1000.000000000000000 ) ;
#121159=DIRECTION ( 'NONE',  ( 1.000000000000000000, 0.000000000000000000, 0.000000000000000000 ) ) ;
#121160=PLANE ( 'NONE',  #65894 ) ;
#121161=DIRECTION ( 'NONE',  ( 0.7071067811865486830, -0.7071067811865464625, -0.000000000000000000 ) ) ;
#121162=VERTEX_POINT ( 'NONE', #4083 ) ;
#121163=CARTESIAN_POINT ( 'NONE',  ( 14.99999999999990230, -10.44781430457071814, 5.000000000000000000 ) ) ;
#121164=DIRECTION ( 'NONE',  ( 1.000000000000000000, -0.000000000000000000, 0.000000000000000000 ) ) ;
#121167=LINE ( 'NONE', #21863, #113398 ) ;
#121168=EDGE_CURVE ( 'NONE', #92202, #138457, #97398, .T. ) ;
#121169=LINE ( 'NONE', #108129, #27476 ) ;
#121170=DIRECTION ( 'NONE',  ( -0.7071067811865487940, 0.7071067811865463515, -0.000000000000000000 ) ) ;
#121171=CARTESIAN_POINT ( 'NONE',  ( -10.01987774928541519, -17.24070752338410273, 20.23474786156467076 ) ) ;
#121172=ORIENTED_EDGE ( 'NONE', *, *, #80644, .T. ) ;
#121173=AXIS2_PLACEMENT_3D ( 'NONE', #67126, #112064, #111320 ) ;
#121174=ORIENTED_EDGE ( 'NONE', *, *, #75699, .T. ) ;
#121175=VERTEX_POINT ( 'NONE', #16421 ) ;
#121176=DIRECTION ( 'NONE',  ( -0.6830127018922180770, -0.6830127018922204085, -0.2588190451025213501 ) ) ;
#121177=CARTESIAN_POINT ( 'NONE',  ( -23.99999999999983302, 9.631307414974306980, -9.079085613539598754 ) ) ;
#121178=ORIENTED_EDGE ( 'NONE', *, *, #75340, .T. ) ;
#121179=EDGE_LOOP ( 'NONE', ( #84956, #119243, #109935, #135831 ) ) ;
#121181=DIRECTION ( 'NONE',  ( -0.6830127018922180770, -0.6830127018922202975, -0.2588190451025213501 ) ) ;
#121183=EDGE_CURVE ( 'NONE', #63923, #37409, #112255, .T. ) ;
#121184=DIRECTION ( 'NONE',  ( 0.6830127018922180770, -0.6830127018922204085, -0.2588190451025213501 ) ) ;
#121186=ORIENTED_EDGE ( 'NONE', *, *, #65192, .F. ) ;
#121187=CARTESIAN_POINT ( 'NONE',  ( 15.18398860626900237, 28.73617430169797871, 5.000000000000000000 ) ) ;
#121188=DIRECTION ( 'NONE',  ( -0.000000000000000000, -0.3543493200069152693, 0.9351131265310292928 ) ) ;
#121190=AXIS2_PLACEMENT_3D ( 'NONE', #38991, #40443, #49892 ) ;
#121191=DIRECTION ( 'NONE',  ( 0.3543493200069162685, -0.000000000000000000, -0.9351131265310288487 ) ) ;
#121192=VERTEX_POINT ( 'NONE', #138963 ) ;
#121194=EDGE_CURVE ( 'NONE', #138878, #49384, #73018, .T. ) ;
#121195=DIRECTION ( 'NONE',  ( -0.6830127018922181881, 0.6830127018922202975, -0.2588190451025214056 ) ) ;
#121196=CARTESIAN_POINT ( 'NONE',  ( -22.82816939922335919, 21.75929247661550647, 4.000000000000000000 ) ) ;
#121197=CARTESIAN_POINT ( 'NONE',  ( 9.524001385854420576, 22.03583458319438293, 4.979811245910088502 ) ) ;
#121199=CARTESIAN_POINT ( 'NONE',  ( 11.99999999999992717, 11.96639925780213964, 5.000000000000000000 ) ) ;
#121200=ORIENTED_EDGE ( 'NONE', *, *, #142397, .T. ) ;
#121202=CARTESIAN_POINT ( 'NONE',  ( 26.99999999999981526, 15.45873954670187977, -0.03131636524300249191 ) ) ;
#121203=CARTESIAN_POINT ( 'NONE',  ( 33.48921356237309510, -27.52281430457078670, 5.000000000000000000 ) ) ;
#121204=DIRECTION ( 'NONE',  ( -0.3543493200069162685, -0.000000000000000000, -0.9351131265310288487 ) ) ;
#121205=ADVANCED_FACE ( 'NONE', ( #15688 ), #26615, .F. ) ;
#121206=VECTOR ( 'NONE', #60022, 1000.000000000000227 ) ;
#121209=CARTESIAN_POINT ( 'NONE',  ( 23.48831394071553547, 6.759292476615649470, 16.35960578974464141 ) ) ;
#121210=ORIENTED_EDGE ( 'NONE', *, *, #53594, .F. ) ;
#121211=PRODUCT_DEFINITION_FORMATION_WITH_SPECIFIED_SOURCE ( 'ANY', '', #54028, .NOT_KNOWN. ) ;
#121212=PLANE ( 'NONE',  #83280 ) ;
#121213=LINE ( 'NONE', #87170, #14523 ) ;
#121214=EDGE_LOOP ( 'NONE', ( #70734, #68708, #29717, #48028 ) ) ;
#121216=LINE ( 'NONE', #140306, #138845 ) ;
#121217=EDGE_LOOP ( 'NONE', ( #39723, #115311, #138077, #76678 ) ) ;
#121218=ORIENTED_EDGE ( 'NONE', *, *, #48582, .T. ) ;
#121220=CARTESIAN_POINT ( 'NONE',  ( -11.20710678118646264, 6.759292476615651246, 5.000000000000000000 ) ) ;
#121221=AXIS2_PLACEMENT_3D ( 'NONE', #139393, #75531, #128489 ) ;
#121222=VERTEX_POINT ( 'NONE', #36765 ) ;
#121223=EDGE_CURVE ( 'NONE', #61200, #134689, #81014, .T. ) ;
#121225=ADVANCED_FACE ( 'NONE', ( #59972 ), #70173, .F. ) ;
#121226=DIRECTION ( 'NONE',  ( 0.7071067811865487940, 0.7071067811865463515, -0.000000000000000000 ) ) ;
#121227=CARTESIAN_POINT ( 'NONE',  ( -30.48921356237309510, -27.52281430457076894, 5.000000000000000000 ) ) ;
#121228=ORIENTED_EDGE ( 'NONE', *, *, #112350, .F. ) ;
#121229=EDGE_CURVE ( 'NONE', #132912, #13889, #137531, .T. ) ;
#121230=CARTESIAN_POINT ( 'NONE',  ( -2.671830600776463172, 17.25929247661555266, 4.000000000000000000 ) ) ;
#121231=PLANE ( 'NONE',  #21216 ) ;
#121232=LINE ( 'NONE', #88634, #14661 ) ;
#121233=LINE ( 'NONE', #131420, #89929 ) ;
#121236=DIRECTION ( 'NONE',  ( 0.7071067811865487940, 0.7071067811865463515, 0.000000000000000000 ) ) ;
#121237=EDGE_CURVE ( 'NONE', #135883, #42588, #27989, .T. ) ;
#121239=ORIENTED_EDGE ( 'NONE', *, *, #75869, .F. ) ;
#121242=ORIENTED_EDGE ( 'NONE', *, *, #108139, .F. ) ;
#121243=EDGE_LOOP ( 'NONE', ( #100555, #60815, #6089, #107956 ) ) ;
#121244=CARTESIAN_POINT ( 'NONE',  ( 34.92499999999998295, 22.22500000000000142, 4.000000000000000000 ) ) ;
#121245=CARTESIAN_POINT ( 'NONE',  ( -17.51078643762690845, -27.52281430457043143, 5.000000000000000000 ) ) ;
#121246=EDGE_CURVE ( 'NONE', #108262, #99716, #54118, .T. ) ;
#121247=ORIENTED_EDGE ( 'NONE', *, *, #29011, .T. ) ;
#121249=CARTESIAN_POINT ( 'NONE',  ( 31.17183060077625356, -2.240707523384262601, 4.000000000000000000 ) ) ;
#121250=VECTOR ( 'NONE', #114776, 1000.000000000000000 ) ;
#121252=ADVANCED_FACE ( 'NONE', ( #139697 ), #96826, .T. ) ;
#121253=LINE ( 'NONE', #88656, #14088 ) ;
#121256=EDGE_CURVE ( 'NONE', #4323, #136798, #53356, .T. ) ;
#121257=FACE_OUTER_BOUND ( 'NONE', #19387, .T. ) ;
#121259=CARTESIAN_POINT ( 'NONE',  ( 1.499999999999992673, 16.77039438581779152, 0.4657186855307696716 ) ) ;
#121261=PLANE ( 'NONE',  #52017 ) ;
#121263=DIRECTION ( 'NONE',  ( 0.7071067811865487940, -0.7071067811865463515, 0.000000000000000000 ) ) ;
#121264=VECTOR ( 'NONE', #43096, 1000.000000000000227 ) ;
#121266=DIRECTION ( 'NONE',  ( 0.6830127018922180770, -0.6830127018922204085, -0.2588190451025213501 ) ) ;
#121267=EDGE_CURVE ( 'NONE', #123220, #25358, #75150, .T. ) ;
#121268=VECTOR ( 'NONE', #89122, 1000.000000000000000 ) ;
#121269=PLANE ( 'NONE',  #32284 ) ;
#121270=VERTEX_POINT ( 'NONE', #84580 ) ;
#121271=ORIENTED_EDGE ( 'NONE', *, *, #98456, .F. ) ;
#121274=DIRECTION ( 'NONE',  ( 0.7071067811865486830, -0.7071067811865464625, -0.000000000000000000 ) ) ;
#121275=VECTOR ( 'NONE', #103397, 999.9999999999998863 ) ;
#121277=ORIENTED_EDGE ( 'NONE', *, *, #72580, .F. ) ;
#121278=ADVANCED_FACE ( 'NONE', ( #130950 ), #117862, .F. ) ;
#121279=FACE_OUTER_BOUND ( 'NONE', #120875, .T. ) ;
#121280=CARTESIAN_POINT ( 'NONE',  ( 20.99451991528748707, 28.92564299267952777, 4.000000000000000000 ) ) ;
#121282=ORIENTED_EDGE ( 'NONE', *, *, #42703, .F. ) ;
#121285=ORIENTED_EDGE ( 'NONE', *, *, #67631, .F. ) ;
#121287=EDGE_CURVE ( 'NONE', #13816, #52532, #57659, .T. ) ;
#121288=FACE_OUTER_BOUND ( 'NONE', #122781, .T. ) ;
#121289=CARTESIAN_POINT ( 'NONE',  ( -36.48921356237310221, -27.52281430457080802, 5.000000000000000000 ) ) ;
#121290=CARTESIAN_POINT ( 'NONE',  ( 21.98155265364317046, 18.75929247661553134, 20.33588619593438196 ) ) ;
#121291=DIRECTION ( 'NONE',  ( 1.000000000000000000, 0.000000000000000000, 0.000000000000000000 ) ) ;
#121292=VERTEX_POINT ( 'NONE', #6951 ) ;
#121293=CARTESIAN_POINT ( 'NONE',  ( -27.48921356237309155, -27.52281430457074762, 5.000000000000000000 ) ) ;
#121295=ORIENTED_EDGE ( 'NONE', *, *, #115290, .T. ) ;
#121299=EDGE_CURVE ( 'NONE', #3326, #30242, #51240, .T. ) ;
#121302=EDGE_LOOP ( 'NONE', ( #114510, #140074, #138166, #48858 ) ) ;
#121306=LINE ( 'NONE', #45919, #23308 ) ;
#121307=FACE_OUTER_BOUND ( 'NONE', #35884, .T. ) ;
#121308=DIRECTION ( 'NONE',  ( -0.6830127018922180770, -0.6830127018922204085, -0.2588190451025213501 ) ) ;
#121309=ORIENTED_EDGE ( 'NONE', *, *, #59524, .T. ) ;
#121311=CARTESIAN_POINT ( 'NONE',  ( 11.20666063542144286, 21.75929247661549937, 4.998822639870701856 ) ) ;
#121312=EDGE_CURVE ( 'NONE', #63081, #132053, #108410, .T. ) ;
#121313=VERTEX_POINT ( 'NONE', #62838 ) ;
#121314=VECTOR ( 'NONE', #138663, 1000.000000000000000 ) ;
#121316=LINE ( 'NONE', #32176, #74509 ) ;
#121317=ORIENTED_EDGE ( 'NONE', *, *, #41090, .T. ) ;
#121318=CARTESIAN_POINT ( 'NONE',  ( 19.49999999999986500, -13.53360074219760101, 5.000000000000000000 ) ) ;
#121319=LINE ( 'NONE', #122747, #101171 ) ;
#121320=LINE ( 'NONE', #54664, #53482 ) ;
#121321=FACE_BOUND ( 'NONE', #56555, .T. ) ;
#121322=CARTESIAN_POINT ( 'NONE',  ( -14.14114973822191423, 6.572112357556697759, 4.331981551378865092 ) ) ;
#121324=LINE ( 'NONE', #44530, #52639 ) ;
#121325=DIRECTION ( 'NONE',  ( -0.6830127018922180770, -0.6830127018922204085, -0.2588190451025213501 ) ) ;
#121326=EDGE_LOOP ( 'NONE', ( #40281, #2972, #54529, #138343 ) ) ;
#121327=VECTOR ( 'NONE', #37386, 1000.000000000000000 ) ;
#121328=FACE_OUTER_BOUND ( 'NONE', #12393, .T. ) ;
#121330=AXIS2_PLACEMENT_3D ( 'NONE', #24804, #77778, #11767 ) ;
#121331=ORIENTED_EDGE ( 'NONE', *, *, #36199, .F. ) ;
#121333=ORIENTED_EDGE ( 'NONE', *, *, #50450, .T. ) ;
#121334=FACE_OUTER_BOUND ( 'NONE', #116861, .T. ) ;
#121335=LINE ( 'NONE', #56131, #62915 ) ;
#121338=CARTESIAN_POINT ( 'NONE',  ( -57.18398860626899705, 28.73617430169827358, 5.000000000000000000 ) ) ;
#121340=DIRECTION ( 'NONE',  ( 1.000000000000000000, 0.000000000000000000, 0.000000000000000000 ) ) ;
#121341=DIRECTION ( 'NONE',  ( -0.6830127018922181881, 0.6830127018922202975, -0.2588190451025214056 ) ) ;
#121342=AXIS2_PLACEMENT_3D ( 'NONE', #55088, #66679, #99259 ) ;
#121343=CARTESIAN_POINT ( 'NONE',  ( -5.999999999999952927, -4.068876922607767455, 4.000000000000000000 ) ) ;
#121344=DIRECTION ( 'NONE',  ( -0.000000000000000000, 0.000000000000000000, 1.000000000000000000 ) ) ;
#121346=ORIENTED_EDGE ( 'NONE', *, *, #93905, .T. ) ;
#121347=ORIENTED_EDGE ( 'NONE', *, *, #16840, .T. ) ;
#121348=DIRECTION ( 'NONE',  ( -0.7071067811865487940, 0.7071067811865463515, 0.000000000000000000 ) ) ;
#121350=ORIENTED_EDGE ( 'NONE', *, *, #135622, .T. ) ;
#121351=ORIENTED_EDGE ( 'NONE', *, *, #9925, .F. ) ;
#121352=AXIS2_PLACEMENT_3D ( 'NONE', #30653, #140799, #8818 ) ;
#121353=EDGE_CURVE ( 'NONE', #103613, #73568, #129481, .T. ) ;
#121355=CARTESIAN_POINT ( 'NONE',  ( 26.99999999999981526, 2.587461875839214720, 4.000000000000000000 ) ) ;
#121356=EDGE_LOOP ( 'NONE', ( #21441, #87119, #7514 ) ) ;
#121357=LINE ( 'NONE', #44569, #16229 ) ;
#121359=EDGE_CURVE ( 'NONE', #61259, #49419, #41780, .T. ) ;
#121360=EDGE_CURVE ( 'NONE', #85633, #51247, #19308, .T. ) ;
#121361=DIRECTION ( 'NONE',  ( 0.7071067811865486830, 0.7071067811865464625, 0.000000000000000000 ) ) ;
#121362=AXIS2_PLACEMENT_3D ( 'NONE', #97277, #41502, #76299 ) ;
#121364=DIRECTION ( 'NONE',  ( -0.000000000000000000, 0.3543493200069153248, 0.9351131265310292928 ) ) ;
#121366=EDGE_CURVE ( 'NONE', #79450, #626, #130228, .T. ) ;
#121368=ORIENTED_EDGE ( 'NONE', *, *, #115404, .F. ) ;
#121369=LINE ( 'NONE', #12608, #3473 ) ;
#121370=CARTESIAN_POINT ( 'NONE',  ( 72.48921356237309510, -27.52281430457106026, 5.000000000000000000 ) ) ;
#121371=ORIENTED_EDGE ( 'NONE', *, *, #455, .T. ) ;
#121373=DIRECTION ( 'NONE',  ( -0.7071067811865487940, 0.7071067811865463515, -0.000000000000000000 ) ) ;
#121374=DIRECTION ( 'NONE',  ( 0.000000000000000000, 0.000000000000000000, -1.000000000000000000 ) ) ;
#121375=CARTESIAN_POINT ( 'NONE',  ( 23.81601139373100295, 28.73617430169770870, 5.000000000000000000 ) ) ;
#121376=EDGE_CURVE ( 'NONE', #19510, #85156, #75843, .T. ) ;
#121378=AXIS2_PLACEMENT_3D ( 'NONE', #8965, #110450, #96023 ) ;
#121380=ORIENTED_EDGE ( 'NONE', *, *, #66738, .F. ) ;
#121381=DIRECTION ( 'NONE',  ( 0.7071067811865487940, 0.7071067811865463515, -0.000000000000000000 ) ) ;
#121382=CARTESIAN_POINT ( 'NONE',  ( 3.299744871391591339, -27.71228299555208352, 4.000000000000000000 ) ) ;
#121383=EDGE_CURVE ( 'NONE', #85323, #93595, #24996, .T. ) ;
#121384=DIRECTION ( 'NONE',  ( -0.000000000000000000, 0.3543493200069153248, 0.9351131265310292928 ) ) ;
#121386=CARTESIAN_POINT ( 'NONE',  ( 16.49999999999988631, -2.568876922607793212, 4.000000000000000000 ) ) ;
#121387=FACE_OUTER_BOUND ( 'NONE', #103499, .T. ) ;
#121388=LINE ( 'NONE', #75075, #96933 ) ;
#121389=EDGE_LOOP ( 'NONE', ( #115683, #72731, #107896, #114523 ) ) ;
#121390=FACE_OUTER_BOUND ( 'NONE', #38074, .T. ) ;
#121391=ORIENTED_EDGE ( 'NONE', *, *, #122322, .T. ) ;
#121394=DIRECTION ( 'NONE',  ( 1.000000000000000000, 0.000000000000000000, 0.000000000000000000 ) ) ;
#121395=CARTESIAN_POINT ( 'NONE',  ( -34.42500000000001137, 21.72500000000000142, 0.5000000000000000000 ) ) ;
#121396=VERTEX_POINT ( 'NONE', #112041 ) ;
#121397=LINE ( 'NONE', #87363, #62274 ) ;
#121398=DIRECTION ( 'NONE',  ( 0.6830127018922180770, -0.6830127018922204085, -0.2588190451025213501 ) ) ;
#121399=DIRECTION ( 'NONE',  ( 0.3543493200069162685, -0.000000000000000000, -0.9351131265310288487 ) ) ;
#121400=ORIENTED_EDGE ( 'NONE', *, *, #60870, .T. ) ;
#121401=EDGE_CURVE ( 'NONE', #39324, #107217, #109881, .T. ) ;
#121403=CARTESIAN_POINT ( 'NONE',  ( 12.29974487139158512, -27.71228299555214747, 4.000000000000000000 ) ) ;
#121405=DIRECTION ( 'NONE',  ( -0.000000000000000000, 0.3543493200069153248, 0.9351131265310292928 ) ) ;
#121407=DIRECTION ( 'NONE',  ( -0.000000000000000000, 0.000000000000000000, 1.000000000000000000 ) ) ;
#121410=DIRECTION ( 'NONE',  ( -0.000000000000000000, -0.3543493200069152693, 0.9351131265310292928 ) ) ;
#121411=EDGE_CURVE ( 'NONE', #100628, #45393, #80145, .T. ) ;
#121412=EDGE_CURVE ( 'NONE', #6385, #95968, #67105, .T. ) ;
#121413=DIRECTION ( 'NONE',  ( -0.7071067811865486830, -0.7071067811865464625, 0.000000000000000000 ) ) ;
#121414=LINE ( 'NONE', #54759, #37157 ) ;
#121415=LINE ( 'NONE', #22777, #108874 ) ;
#121416=ORIENTED_EDGE ( 'NONE', *, *, #124245, .T. ) ;
#121417=CARTESIAN_POINT ( 'NONE',  ( -5.206660635421487271, 21.75929247661549937, 4.998822639870708073 ) ) ;
#121418=EDGE_LOOP ( 'NONE', ( #20172, #93487, #47259, #126067 ) ) ;
#121419=CARTESIAN_POINT ( 'NONE',  ( -24.29974487139158867, -27.71228299555223273, 4.000000000000000000 ) ) ;
#121420=DIRECTION ( 'NONE',  ( 0.7071067811865487940, -0.7071067811865463515, 0.000000000000000000 ) ) ;
#121422=CARTESIAN_POINT ( 'NONE',  ( 30.32816939922332367, 20.25929247661551003, 4.000000000000000000 ) ) ;
#121423=CARTESIAN_POINT ( 'NONE',  ( 69.48921356237309510, -27.52281430457103895, 5.000000000000000000 ) ) ;
#121425=EDGE_CURVE ( 'NONE', #31789, #139138, #110568, .T. ) ;
#121426=LINE ( 'NONE', #101099, #27868 ) ;
#121428=ORIENTED_EDGE ( 'NONE', *, *, #92658, .T. ) ;
#121429=EDGE_LOOP ( 'NONE', ( #133258, #96485, #81487, #119495 ) ) ;
#121430=CARTESIAN_POINT ( 'NONE',  ( 17.51078643762690845, -27.52281430457043143, 5.000000000000000000 ) ) ;
#121434=CARTESIAN_POINT ( 'NONE',  ( -24.32816939922336275, -12.74070752338415602, 4.000000000000000000 ) ) ;
#121435=CARTESIAN_POINT ( 'NONE',  ( 23.99451991528749062, 28.92564299267954908, 4.000000000000000000 ) ) ;
#121437=DIRECTION ( 'NONE',  ( -0.7071067811865486830, 0.7071067811865464625, 0.000000000000000000 ) ) ;
#121438=AXIS2_PLACEMENT_3D ( 'NONE', #76917, #12329, #43542 ) ;
#121439=CARTESIAN_POINT ( 'NONE',  ( 34.92499999999998295, -22.22500000000000142, 4.500000000000000888 ) ) ;
#121440=ORIENTED_EDGE ( 'NONE', *, *, #1519, .F. ) ;
#121442=EDGE_CURVE ( 'NONE', #68957, #3959, #22835, .T. ) ;
#121443=PLANE ( 'NONE',  #74747 ) ;
#121444=VECTOR ( 'NONE', #132170, 1000.000000000000000 ) ;
#121445=DIRECTION ( 'NONE',  ( 0.3543493200069162685, -0.000000000000000000, -0.9351131265310288487 ) ) ;
#121447=EDGE_LOOP ( 'NONE', ( #114173, #14313, #53232, #113171 ) ) ;
#121448=EDGE_CURVE ( 'NONE', #85002, #77505, #72497, .T. ) ;
#121449=LINE ( 'NONE', #31604, #14330 ) ;
#121450=VERTEX_POINT ( 'NONE', #44677 ) ;
#121452=CARTESIAN_POINT ( 'NONE',  ( -4.396568071053548188, -14.24070752338413648, 19.24067776001725250 ) ) ;
#121454=ORIENTED_EDGE ( 'NONE', *, *, #24593, .F. ) ;
#121455=DIRECTION ( 'NONE',  ( -0.6830127018922180770, -0.6830127018922204085, -0.2588190451025213501 ) ) ;
#121457=DIRECTION ( 'NONE',  ( -0.7071067811865486830, -0.7071067811865464625, 0.000000000000000000 ) ) ;
#121458=DIRECTION ( 'NONE',  ( 0.7071067811865486830, -0.7071067811865464625, -0.000000000000000000 ) ) ;
#121459=DIRECTION ( 'NONE',  ( -0.7071067811865486830, -0.7071067811865464625, 0.000000000000000000 ) ) ;
#121460=DIRECTION ( 'NONE',  ( -0.3543493200069163240, -0.000000000000000000, -0.9351131265310288487 ) ) ;
#121461=EDGE_LOOP ( 'NONE', ( #66434, #121186, #79998, #70896 ) ) ;
#121462=FACE_OUTER_BOUND ( 'NONE', #26166, .T. ) ;
#121463=PLANE ( 'NONE',  #123513 ) ;
#121464=FACE_OUTER_BOUND ( 'NONE', #142577, .T. ) ;
#121465=ORIENTED_EDGE ( 'NONE', *, *, #32094, .F. ) ;
#121466=VECTOR ( 'NONE', #88120, 1000.000000000000000 ) ;
#121467=EDGE_CURVE ( 'NONE', #125463, #138848, #34470, .T. ) ;
#121468=EDGE_LOOP ( 'NONE', ( #33539, #90354, #93421, #88613 ) ) ;
#121470=AXIS2_PLACEMENT_3D ( 'NONE', #113648, #14348, #58632 ) ;
#121471=VECTOR ( 'NONE', #69547, 1000.000000000000000 ) ;
#121472=VERTEX_POINT ( 'NONE', #88871 ) ;
#121474=DIRECTION ( 'NONE',  ( -0.7071067811865486830, 0.7071067811865464625, 0.000000000000000000 ) ) ;
#121475=CARTESIAN_POINT ( 'NONE',  ( -1.499999999999984013, -4.912538124160710673, 4.000000000000000000 ) ) ;
#121476=CARTESIAN_POINT ( 'NONE',  ( 30.48921356237309510, -27.52281430457076894, 5.000000000000000000 ) ) ;
#121477=CARTESIAN_POINT ( 'NONE',  ( -9.328169399223467551, 11.25929247661560240, 4.000000000000000000 ) ) ;
#121478=PLANE ( 'NONE',  #110358 ) ;
#121479=ORIENTED_EDGE ( 'NONE', *, *, #71199, .T. ) ;
#121480=ORIENTED_EDGE ( 'NONE', *, *, #66494, .T. ) ;
#121484=DIRECTION ( 'NONE',  ( -0.7071067811865486830, -0.7071067811865464625, -0.000000000000000000 ) ) ;
#121485=CARTESIAN_POINT ( 'NONE',  ( 23.30673006690386728, -3.740707523384244837, 12.88036043432862243 ) ) ;
#121486=PLANE ( 'NONE',  #109502 ) ;
#121487=ORIENTED_EDGE ( 'NONE', *, *, #80699, .F. ) ;
#121488=FACE_OUTER_BOUND ( 'NONE', #94266, .T. ) ;
#121489=DIRECTION ( 'NONE',  ( -0.7071067811865486830, -0.7071067811865464625, 0.000000000000000000 ) ) ;
#121496=ORIENTED_EDGE ( 'NONE', *, *, #57373, .T. ) ;
#121498=ORIENTED_EDGE ( 'NONE', *, *, #116671, .F. ) ;
#121499=VERTEX_POINT ( 'NONE', #88147 ) ;
#121500=DIRECTION ( 'NONE',  ( -0.000000000000000000, -0.000000000000000000, 1.000000000000000000 ) ) ;
#121502=CARTESIAN_POINT ( 'NONE',  ( 11.99999999999991296, -8.151047557385055597, -8.977947279169828931 ) ) ;
#121506=CARTESIAN_POINT ( 'NONE',  ( 0.000000000000000000, 0.000000000000000000, 5.000000000000000000 ) ) ;
#121508=ADVANCED_FACE ( 'NONE', ( #56965 ), #98991, .F. ) ;
#121509=LINE ( 'NONE', #66452, #94376 ) ;
#121510=CARTESIAN_POINT ( 'NONE',  ( -42.18398860626899705, 28.73617430169816700, 5.000000000000000000 ) ) ;
#121511=EDGE_CURVE ( 'NONE', #91841, #41843, #122166, .T. ) ;
#121512=CARTESIAN_POINT ( 'NONE',  ( 11.51078643762690490, -27.52281430457047406, 5.000000000000000000 ) ) ;
#121513=ADVANCED_FACE ( 'NONE', ( #121462 ), #100444, .T. ) ;
#121514=FACE_OUTER_BOUND ( 'NONE', #141787, .T. ) ;
#121515=EDGE_LOOP ( 'NONE', ( #140190, #93209, #51591, #140085 ) ) ;
#121516=DIRECTION ( 'NONE',  ( -0.7071067811865487940, 0.7071067811865463515, 0.000000000000000000 ) ) ;
#121517=DIRECTION ( 'NONE',  ( -0.000000000000000000, 0.000000000000000000, 1.000000000000000000 ) ) ;
#121518=ADVANCED_FACE ( 'NONE', ( #123648 ), #66398, .F. ) ;
#121519=ORIENTED_EDGE ( 'NONE', *, *, #37258, .F. ) ;
#121522=ADVANCED_FACE ( 'NONE', ( #101138 ), #133785, .F. ) ;
#121523=ORIENTED_EDGE ( 'NONE', *, *, #133885, .T. ) ;
#121525=ORIENTED_EDGE ( 'NONE', *, *, #39422, .F. ) ;
#121527=EDGE_CURVE ( 'NONE', #46199, #85411, #38750, .T. ) ;
#121528=FACE_OUTER_BOUND ( 'NONE', #66461, .T. ) ;
#121529=AXIS2_PLACEMENT_3D ( 'NONE', #47695, #35386, #49102 ) ;
#121532=CARTESIAN_POINT ( 'NONE',  ( 30.70701326429282929, -21.74070752338406365, 4.999753212805224223 ) ) ;
#121533=AXIS2_PLACEMENT_3D ( 'NONE', #4412, #135725, #125575 ) ;
#121534=ADVANCED_FACE ( 'NONE', ( #105413 ), #116305, .F. ) ;
#121536=FACE_OUTER_BOUND ( 'NONE', #4394, .T. ) ;
#121537=DIRECTION ( 'NONE',  ( 1.000000000000000000, 0.000000000000000000, 0.000000000000000000 ) ) ;
#121539=LINE ( 'NONE', #90348, #14323 ) ;
#121540=LINE ( 'NONE', #88223, #142401 ) ;
#121541=ADVANCED_FACE ( 'NONE', ( #113433 ), #16999, .T. ) ;
#121542=ORIENTED_EDGE ( 'NONE', *, *, #67771, .F. ) ;
#121543=DIRECTION ( 'NONE',  ( -0.000000000000000000, -0.3543493200069152693, 0.9351131265310292928 ) ) ;
#121544=VECTOR ( 'NONE', #15818, 999.9999999999998863 ) ;
#121548=ORIENTED_EDGE ( 'NONE', *, *, #19629, .F. ) ;
#121552=DIRECTION ( 'NONE',  ( 1.000000000000000000, 0.000000000000000000, 0.000000000000000000 ) ) ;
#121553=ORIENTED_EDGE ( 'NONE', *, *, #44094, .F. ) ;
#121554=LINE ( 'NONE', #87518, #65029 ) ;
#121555=ORIENTED_EDGE ( 'NONE', *, *, #37070, .T. ) ;
#121558=VECTOR ( 'NONE', #50426, 1000.000000000000000 ) ;
#121560=CARTESIAN_POINT ( 'NONE',  ( -11.51078643762690490, -27.52281430457047406, 5.000000000000000000 ) ) ;
#121563=VECTOR ( 'NONE', #47777, 1000.000000000000000 ) ;
#121566=ORIENTED_EDGE ( 'NONE', *, *, #43042, .T. ) ;
#121567=EDGE_CURVE ( 'NONE', #76029, #69406, #69996, .T. ) ;
#121570=CARTESIAN_POINT ( 'NONE',  ( -6.489213562373093325, -27.52281430457059841, 5.000000000000000000 ) ) ;
#121571=FACE_OUTER_BOUND ( 'NONE', #15963, .T. ) ;
#121573=LINE ( 'NONE', #56382, #124795 ) ;
#121575=DIRECTION ( 'NONE',  ( 0.7071067811865486830, -0.7071067811865464625, -0.000000000000000000 ) ) ;
#121576=CARTESIAN_POINT ( 'NONE',  ( -20.51078643762690490, -27.52281430457041012, 5.000000000000000000 ) ) ;
#121577=EDGE_CURVE ( 'NONE', #60821, #1343, #50348, .T. ) ;
#121578=ORIENTED_EDGE ( 'NONE', *, *, #45677, .F. ) ;
#121579=CARTESIAN_POINT ( 'NONE',  ( -32.99999999999976552, -10.44781430457071991, 5.000000000000000000 ) ) ;
#121580=ORIENTED_EDGE ( 'NONE', *, *, #8265, .F. ) ;
#121582=VERTEX_POINT ( 'NONE', #136618 ) ;
#121583=ADVANCED_FACE ( 'NONE', ( #60536 ), #125037, .F. ) ;
#121585=CARTESIAN_POINT ( 'NONE',  ( -16.49999999999988276, -1.592773361805376098, -6.492772025301186467 ) ) ;
#121586=CARTESIAN_POINT ( 'NONE',  ( -27.18398860626900060, 28.73617430169806042, 5.000000000000000000 ) ) ;
#121587=ORIENTED_EDGE ( 'NONE', *, *, #38489, .F. ) ;
#121588=LINE ( 'NONE', #77423, #35359 ) ;
#121589=ORIENTED_EDGE ( 'NONE', *, *, #30395, .F. ) ;
#121590=ORIENTED_EDGE ( 'NONE', *, *, #20592, .T. ) ;
#121591=CARTESIAN_POINT ( 'NONE',  ( -24.18398860626899705, 28.73617430169804265, 5.000000000000000000 ) ) ;
#121593=ORIENTED_EDGE ( 'NONE', *, *, #96225, .T. ) ;
#121594=ADVANCED_FACE ( 'NONE', ( #27149 ), #82277, .F. ) ;
#121595=CARTESIAN_POINT ( 'NONE',  ( 22.93003974513577603, -0.7407075233842735917, 13.87443053587605490 ) ) ;
#121598=LINE ( 'NONE', #107852, #6558 ) ;
#121599=ADVANCED_FACE ( 'NONE', ( #135920 ), #93837, .F. ) ;
#121600=CARTESIAN_POINT ( 'NONE',  ( -31.49999999999977973, -13.91253812416061386, 4.000000000000000000 ) ) ;
#121601=LINE ( 'NONE', #131071, #136384 ) ;
#121605=CARTESIAN_POINT ( 'NONE',  ( -27.48921356237309155, -27.52281430457074762, 5.000000000000000000 ) ) ;
#121606=VERTEX_POINT ( 'NONE', #127171 ) ;
#121608=CARTESIAN_POINT ( 'NONE',  ( 15.70710678118643422, 20.25929247661551003, 5.000000000000000000 ) ) ;
#121609=ORIENTED_EDGE ( 'NONE', *, *, #87957, .T. ) ;
#121610=EDGE_CURVE ( 'NONE', #98423, #110210, #70697, .T. ) ;
#121611=PLANE ( 'NONE',  #110215 ) ;
#121612=CARTESIAN_POINT ( 'NONE',  ( -31.17183060077624646, -17.24070752338410273, 4.000000000000000000 ) ) ;
#121613=DIRECTION ( 'NONE',  ( -0.000000000000000000, 0.3543493200069153248, 0.9351131265310292928 ) ) ;
#121615=EDGE_LOOP ( 'NONE', ( #44105, #130217, #50991, #87796 ) ) ;
#121616=DIRECTION ( 'NONE',  ( 0.7071067811865487940, 0.7071067811865463515, 0.000000000000000000 ) ) ;
#121617=LINE ( 'NONE', #78148, #141476 ) ;
#121618=FACE_OUTER_BOUND ( 'NONE', #66931, .T. ) ;
#121619=EDGE_CURVE ( 'NONE', #135612, #21613, #92389, .T. ) ;
#121621=DIRECTION ( 'NONE',  ( -0.000000000000000000, -0.000000000000000000, 1.000000000000000000 ) ) ;
#121622=DIRECTION ( 'NONE',  ( 0.7071067811865486830, -0.7071067811865464625, -0.000000000000000000 ) ) ;
#121623=ORIENTED_EDGE ( 'NONE', *, *, #83391, .F. ) ;
#121624=CARTESIAN_POINT ( 'NONE',  ( 28.82816939922332722, 21.75929247661549581, 4.000000000000000000 ) ) ;
#121625=DIRECTION ( 'NONE',  ( -0.7071067811865486830, -0.7071067811865464625, 0.000000000000000000 ) ) ;
#121626=CARTESIAN_POINT ( 'NONE',  ( 36.48921356237310221, -27.52281430457080802, 5.000000000000000000 ) ) ;
#121627=LINE ( 'NONE', #23012, #132585 ) ;
#121628=ORIENTED_EDGE ( 'NONE', *, *, #98340, .T. ) ;
#121629=VECTOR ( 'NONE', #80843, 1000.000000000000227 ) ;
#121630=ORIENTED_EDGE ( 'NONE', *, *, #131088, .T. ) ;
#121631=ORIENTED_EDGE ( 'NONE', *, *, #110862, .F. ) ;
#121633=EDGE_LOOP ( 'NONE', ( #75622, #8806, #114297, #26215 ) ) ;
#121634=VECTOR ( 'NONE', #88155, 1000.000000000000000 ) ;
#121635=DIRECTION ( 'NONE',  ( 0.7071067811865486830, -0.7071067811865464625, -0.000000000000000000 ) ) ;
#121636=CARTESIAN_POINT ( 'NONE',  ( -27.48921356237309155, -27.52281430457074762, 5.000000000000000000 ) ) ;
#121637=DIRECTION ( 'NONE',  ( 0.6830127018922180770, -0.6830127018922204085, -0.2588190451025213501 ) ) ;
#121638=DIRECTION ( 'NONE',  ( -0.7071067811865486830, 0.7071067811865463515, 0.000000000000000000 ) ) ;
#121639=EDGE_LOOP ( 'NONE', ( #8286, #103922, #55425, #3597 ) ) ;
#121640=CARTESIAN_POINT ( 'NONE',  ( -16.40128505106373780, 22.22500000000000142, 12.01932804697904800 ) ) ;
#121642=EDGE_CURVE ( 'NONE', #136740, #98772, #81571, .T. ) ;
#121644=EDGE_CURVE ( 'NONE', #15282, #32517, #114847, .T. ) ;
#121649=EDGE_LOOP ( 'NONE', ( #51136, #116200, #34865, #27749 ) ) ;
#121650=ORIENTED_EDGE ( 'NONE', *, *, #81954, .T. ) ;
#121651=ORIENTED_EDGE ( 'NONE', *, *, #56782, .T. ) ;
#121652=FACE_OUTER_BOUND ( 'NONE', #3743, .T. ) ;
#121653=EDGE_CURVE ( 'NONE', #35333, #107292, #98136, .T. ) ;
#121654=DIRECTION ( 'NONE',  ( 0.7071067811865486830, -0.7071067811865464625, -0.000000000000000000 ) ) ;
#121655=CARTESIAN_POINT ( 'NONE',  ( 22.82816939922337340, -8.240707523384203981, 4.000000000000000000 ) ) ;
#121656=DIRECTION ( 'NONE',  ( 0.6830127018922180770, -0.6830127018922204085, -0.2588190451025213501 ) ) ;
#121657=VECTOR ( 'NONE', #125398, 1000.000000000000227 ) ;
#121658=CARTESIAN_POINT ( 'NONE',  ( 14.99451991528749595, 28.92564299267948513, 4.000000000000000000 ) ) ;
#121660=( LENGTH_UNIT ( ) NAMED_UNIT ( * ) SI_UNIT ( .MILLI., .METRE. ) );
#121661=VECTOR ( 'NONE', #63017, 999.9999999999998863 ) ;
#121662=VERTEX_POINT ( 'NONE', #106845 ) ;
#121663=VECTOR ( 'NONE', #57399, 999.9999999999998863 ) ;
#121664=ORIENTED_EDGE ( 'NONE', *, *, #140890, .F. ) ;
#121666=VERTEX_POINT ( 'NONE', #85102 ) ;
#121667=ORIENTED_EDGE ( 'NONE', *, *, #79391, .F. ) ;
#121668=FACE_OUTER_BOUND ( 'NONE', #32347, .T. ) ;
#121670=CARTESIAN_POINT ( 'NONE',  ( -33.48921356237309510, -27.52281430457078670, 5.000000000000000000 ) ) ;
#121671=DIRECTION ( 'NONE',  ( -0.000000000000000000, 0.3543493200069153248, 0.9351131265310292928 ) ) ;
#121672=CARTESIAN_POINT ( 'NONE',  ( 15.29974487139158867, -27.71228299555216879, 4.000000000000000000 ) ) ;
#121673=LINE ( 'NONE', #54336, #136342 ) ;
#121675=ORIENTED_EDGE ( 'NONE', *, *, #91513, .F. ) ;
#121677=VERTEX_POINT ( 'NONE', #97379 ) ;
#121678=CARTESIAN_POINT ( 'NONE',  ( 32.99451991528749062, 28.92564299267960948, 4.000000000000000000 ) ) ;
#121679=ORIENTED_EDGE ( 'NONE', *, *, #115738, .T. ) ;
#121680=CARTESIAN_POINT ( 'NONE',  ( -34.92500000000001137, 15.85612307739227944, 4.000000000000000000 ) ) ;
#121681=ADVANCED_FACE ( 'NONE', ( #75671 ), #30751, .F. ) ;
#121684=DIRECTION ( 'NONE',  ( 0.7071067811865486830, -0.7071067811865464625, -0.000000000000000000 ) ) ;
#121685=ORIENTED_EDGE ( 'NONE', *, *, #63146, .T. ) ;
#121686=ORIENTED_EDGE ( 'NONE', *, *, #95006, .F. ) ;
#121687=ORIENTED_EDGE ( 'NONE', *, *, #11058, .F. ) ;
#121688=EDGE_CURVE ( 'NONE', #89682, #41509, #64796, .T. ) ;
#121689=EDGE_CURVE ( 'NONE', #77053, #13854, #118434, .T. ) ;
#121690=LINE ( 'NONE', #45616, #141454 ) ;
#121691=DIRECTION ( 'NONE',  ( -0.7071067811865486830, 0.7071067811865464625, 0.000000000000000000 ) ) ;
#121692=EDGE_CURVE ( 'NONE', #113754, #88854, #142361, .T. ) ;
#121695=EDGE_CURVE ( 'NONE', #373, #42048, #17680, .T. ) ;
#121696=CARTESIAN_POINT ( 'NONE',  ( 11.35681257248254106, -20.24070752338407431, 21.22881796311215652 ) ) ;
#121698=EDGE_CURVE ( 'NONE', #109084, #81908, #41594, .T. ) ;
#121699=CARTESIAN_POINT ( 'NONE',  ( 34.57058949319513630, 22.20469455417148907, 4.123089426795141677 ) ) ;
#121700=DIRECTION ( 'NONE',  ( 0.7071067811865487940, 0.7071067811865463515, -0.000000000000000000 ) ) ;
#121701=EDGE_CURVE ( 'NONE', #98903, #112793, #43051, .T. ) ;
#121704=DIRECTION ( 'NONE',  ( 0.7071067811865487940, 0.7071067811865463515, 0.000000000000000000 ) ) ;
#121705=ORIENTED_EDGE ( 'NONE', *, *, #30439, .T. ) ;
#121707=VERTEX_POINT ( 'NONE', #130050 ) ;
#121708=DIRECTION ( 'NONE',  ( -0.7071067811865486830, -0.7071067811865464625, 0.000000000000000000 ) ) ;
#121709=VERTEX_POINT ( 'NONE', #51062 ) ;
#121710=VERTEX_POINT ( 'NONE', #19835 ) ;
#121711=CARTESIAN_POINT ( 'NONE',  ( 30.32816939922331656, 14.25929247661557042, 4.000000000000000000 ) ) ;
#121712=CARTESIAN_POINT ( 'NONE',  ( -30.48921356237309510, -27.52281430457076894, 5.000000000000000000 ) ) ;
#121713=LINE ( 'NONE', #91953, #117331 ) ;
#121714=EDGE_CURVE ( 'NONE', #109897, #5522, #28603, .T. ) ;
#121715=ADVANCED_FACE ( 'NONE', ( #64076 ), #72858, .F. ) ;
#121717=CARTESIAN_POINT ( 'NONE',  ( -4.499999999999970690, 0.4311230773921797543, 4.000000000000000000 ) ) ;
#121718=ORIENTED_EDGE ( 'NONE', *, *, #13209, .F. ) ;
#121719=FACE_OUTER_BOUND ( 'NONE', #109173, .T. ) ;
#121720=ORIENTED_EDGE ( 'NONE', *, *, #36890, .F. ) ;
#121724=AXIS2_PLACEMENT_3D ( 'NONE', #59469, #50006, #81947 ) ;
#121726=ORIENTED_EDGE ( 'NONE', *, *, #22857, .T. ) ;
#121729=FACE_OUTER_BOUND ( 'NONE', #2890, .T. ) ;
#121730=ORIENTED_EDGE ( 'NONE', *, *, #75768, .F. ) ;
#121731=ORIENTED_EDGE ( 'NONE', *, *, #8245, .T. ) ;
#121732=VERTEX_POINT ( 'NONE', #106109 ) ;
#121733=FACE_OUTER_BOUND ( 'NONE', #91166, .T. ) ;
#121735=DIRECTION ( 'NONE',  ( 0.7071067811865487940, 0.7071067811865463515, -0.000000000000000000 ) ) ;
#121737=LINE ( 'NONE', #23119, #45058 ) ;
#121738=DIRECTION ( 'NONE',  ( 0.7071067811865486830, -0.7071067811865464625, -0.000000000000000000 ) ) ;
#121739=EDGE_LOOP ( 'NONE', ( #53471, #10479, #19266, #24407 ) ) ;
#121740=LINE ( 'NONE', #57254, #122107 ) ;
#121741=VECTOR ( 'NONE', #90973, 999.9999999999998863 ) ;
#121742=CARTESIAN_POINT ( 'NONE',  ( -34.92500000000001137, -22.22500000000000142, 4.000000000000000000 ) ) ;
#121743=DIRECTION ( 'NONE',  ( -0.7071067811865486830, -0.7071067811865464625, 0.000000000000000000 ) ) ;
#121744=EDGE_CURVE ( 'NONE', #56146, #104888, #87272, .T. ) ;
#121745=VERTEX_POINT ( 'NONE', #40212 ) ;
#121747=DIRECTION ( 'NONE',  ( 0.6830127018922180770, -0.6830127018922204085, -0.2588190451025213501 ) ) ;
#121748=ORIENTED_EDGE ( 'NONE', *, *, #26823, .F. ) ;
#121749=LINE ( 'NONE', #31207, #90286 ) ;
#121750=ORIENTED_EDGE ( 'NONE', *, *, #6383, .T. ) ;
#121751=ORIENTED_EDGE ( 'NONE', *, *, #112688, .F. ) ;
#121752=CARTESIAN_POINT ( 'NONE',  ( -9.489213562373095101, -27.52281430457062328, 5.000000000000000000 ) ) ;
#121753=CARTESIAN_POINT ( 'NONE',  ( 0.7071067811865450192, 5.259292476615662792, 5.000000000000000000 ) ) ;
#121755=CARTESIAN_POINT ( 'NONE',  ( -34.92500000000001137, 8.718490437204135191, 4.759050581649341360 ) ) ;
#121759=FACE_OUTER_BOUND ( 'NONE', #121447, .T. ) ;
#121760=VECTOR ( 'NONE', #27857, 1000.000000000000227 ) ;
#121761=DIRECTION ( 'NONE',  ( 0.7071067811865487940, -0.7071067811865463515, 0.000000000000000000 ) ) ;
#121762=DIRECTION ( 'NONE',  ( 0.7071067811865486830, -0.7071067811865464625, -0.000000000000000000 ) ) ;
#121763=CYLINDRICAL_SURFACE ( 'NONE', #11866, 0.5000000000000000000 ) ;
#121764=AXIS2_PLACEMENT_3D ( 'NONE', #118224, #104509, #61753 ) ;
#121765=EDGE_CURVE ( 'NONE', #60839, #43089, #52465, .T. ) ;
#121767=DIRECTION ( 'NONE',  ( 0.3543493200069162685, -0.000000000000000000, -0.9351131265310288487 ) ) ;
#121768=CARTESIAN_POINT ( 'NONE',  ( -78.48921356237309510, -27.52281430457109934, 5.000000000000000000 ) ) ;
#121770=DIRECTION ( 'NONE',  ( -0.7071067811865486830, 0.7071067811865464625, 0.000000000000000000 ) ) ;
#121771=CARTESIAN_POINT ( 'NONE',  ( 35.14818355038124054, 17.25929247661554200, 8.802941693769282594 ) ) ;
#121774=LINE ( 'NONE', #22450, #91678 ) ;
#121775=ORIENTED_EDGE ( 'NONE', *, *, #80106, .F. ) ;
#121778=VERTEX_POINT ( 'NONE', #108242 ) ;
#121779=ORIENTED_EDGE ( 'NONE', *, *, #56043, .T. ) ;
#121780=EDGE_CURVE ( 'NONE', #43690, #134514, #8910, .T. ) ;
#121781=ORIENTED_EDGE ( 'NONE', *, *, #65201, .T. ) ;
#121783=CARTESIAN_POINT ( 'NONE',  ( 0.000000000000000000, 0.000000000000000000, 5.000000000000000000 ) ) ;
#121784=ORIENTED_EDGE ( 'NONE', *, *, #67446, .F. ) ;
#121785=CARTESIAN_POINT ( 'NONE',  ( 8.700255128608413102, -27.71228299555199825, 4.000000000000000000 ) ) ;
#121786=CARTESIAN_POINT ( 'NONE',  ( 24.18398860626899705, 28.73617430169804265, 5.000000000000000000 ) ) ;
#121787=CARTESIAN_POINT ( 'NONE',  ( 0.000000000000000000, 0.000000000000000000, 5.000000000000000000 ) ) ;
#121788=LINE ( 'NONE', #43539, #102183 ) ;
#121790=ORIENTED_EDGE ( 'NONE', *, *, #47766, .F. ) ;
#121791=DIRECTION ( 'NONE',  ( -0.000000000000000000, 0.000000000000000000, 1.000000000000000000 ) ) ;
#121792=FACE_OUTER_BOUND ( 'NONE', #17357, .T. ) ;
#121793=CARTESIAN_POINT ( 'NONE',  ( 4.526428939989314948, -22.22500000000000142, -9.949621197219423507 ) ) ;
#121794=CARTESIAN_POINT ( 'NONE',  ( -17.29289321881333308, 14.25929247661557042, 5.000000000000000000 ) ) ;
#121795=DIRECTION ( 'NONE',  ( -0.7071067811865487940, 0.7071067811865463515, -0.000000000000000000 ) ) ;
#121798=EDGE_CURVE ( 'NONE', #141085, #19388, #99527, .T. ) ;
#121799=VERTEX_POINT ( 'NONE', #57501 ) ;
#121800=EDGE_LOOP ( 'NONE', ( #19579, #132921, #142447, #139542 ) ) ;
#121802=ORIENTED_EDGE ( 'NONE', *, *, #80787, .T. ) ;
#121804=CARTESIAN_POINT ( 'NONE',  ( 42.48921356237308800, -27.52281430457085065, 5.000000000000000000 ) ) ;
#121805=VECTOR ( 'NONE', #80995, 1000.000000000000000 ) ;
#121807=CARTESIAN_POINT ( 'NONE',  ( -69.48921356237309510, -27.52281430457103895, 5.000000000000000000 ) ) ;
#121808=DIRECTION ( 'NONE',  ( -0.000000000000000000, -1.000000000000000000, -0.000000000000000000 ) ) ;
#121809=ADVANCED_FACE ( 'NONE', ( #66229 ), #13232, .F. ) ;
#121811=EDGE_CURVE ( 'NONE', #32452, #61250, #121996, .T. ) ;
#121813=VERTEX_POINT ( 'NONE', #44499 ) ;
#121814=AXIS2_PLACEMENT_3D ( 'NONE', #103924, #40168, #95213 ) ;
#121815=PLANE ( 'NONE',  #67070 ) ;
#121821=DIRECTION ( 'NONE',  ( 0.7071067811865487940, -0.7071067811865463515, 0.000000000000000000 ) ) ;
#121823=CARTESIAN_POINT ( 'NONE',  ( -5.816011393731002066, 28.73617430169783304, 5.000000000000000000 ) ) ;
#121824=CARTESIAN_POINT ( 'NONE',  ( -48.48921356237309510, -27.52281430457089328, 5.000000000000000000 ) ) ;
#121826=ORIENTED_EDGE ( 'NONE', *, *, #103222, .F. ) ;
#121827=VECTOR ( 'NONE', #58625, 1000.000000000000227 ) ;
#121828=DIRECTION ( 'NONE',  ( -0.6830127018922180770, -0.6830127018922204085, -0.2588190451025213501 ) ) ;
#121830=ORIENTED_EDGE ( 'NONE', *, *, #135199, .F. ) ;
#121831=ORIENTED_EDGE ( 'NONE', *, *, #76577, .T. ) ;
#121833=LINE ( 'NONE', #78368, #136767 ) ;
#121834=ORIENTED_EDGE ( 'NONE', *, *, #110283, .T. ) ;
#121835=DIRECTION ( 'NONE',  ( 0.6830127018922180770, -0.6830127018922204085, -0.2588190451025213501 ) ) ;
#121837=DIRECTION ( 'NONE',  ( -0.000000000000000000, 0.3543493200069153248, 0.9351131265310292928 ) ) ;
#121838=CARTESIAN_POINT ( 'NONE',  ( 0.000000000000000000, 0.000000000000000000, 5.000000000000000000 ) ) ;
#121839=LINE ( 'NONE', #22521, #34980 ) ;
#121840=AXIS2_PLACEMENT_3D ( 'NONE', #572, #44870, #89054 ) ;
#121841=FACE_BOUND ( 'NONE', #12350, .T. ) ;
#121843=LINE ( 'NONE', #41, #131376 ) ;
#121844=CARTESIAN_POINT ( 'NONE',  ( 9.183988606268997046, 28.73617430169793607, 5.000000000000000000 ) ) ;
#121845=CARTESIAN_POINT ( 'NONE',  ( 34.92499999999998295, -11.24070752338416490, 4.255531930566169407 ) ) ;
#121846=ORIENTED_EDGE ( 'NONE', *, *, #94563, .F. ) ;
#121848=ORIENTED_EDGE ( 'NONE', *, *, #26127, .T. ) ;
#121852=ORIENTED_EDGE ( 'NONE', *, *, #93396, .T. ) ;
#121853=VECTOR ( 'NONE', #8233, 1000.000000000000000 ) ;
#121854=VECTOR ( 'NONE', #122275, 1000.000000000000000 ) ;
#121855=ADVANCED_FACE ( 'NONE', ( #43747 ), #23405, .F. ) ;
#121857=VERTEX_POINT ( 'NONE', #24141 ) ;
#121858=DIRECTION ( 'NONE',  ( 0.7071067811865486830, -0.7071067811865464625, -0.000000000000000000 ) ) ;
#121859=ADVANCED_FACE ( 'NONE', ( #65540 ), #100276, .F. ) ;
#121861=CARTESIAN_POINT ( 'NONE',  ( 25.49999999999982947, 0.4497235411627699131, -5.599840258123482073 ) ) ;
#121862=VERTEX_POINT ( 'NONE', #45215 ) ;
#121863=EDGE_CURVE ( 'NONE', #5696, #117806, #111869, .T. ) ;
#121864=CARTESIAN_POINT ( 'NONE',  ( 0.5240013858544890768, 22.03583458319437938, 4.979811245910086726 ) ) ;
#121865=PLANE ( 'NONE',  #80537 ) ;
#121867=ADVANCED_FACE ( 'NONE', ( #67682 ), #12532, .F. ) ;
#121868=DIRECTION ( 'NONE',  ( -0.7071067811865486830, -0.7071067811865464625, -0.000000000000000000 ) ) ;
#121869=DIRECTION ( 'NONE',  ( -0.7071067811865486830, -0.7071067811865464625, 0.000000000000000000 ) ) ;
#121870=DIRECTION ( 'NONE',  ( 0.6830127018922180770, -0.6830127018922204085, -0.2588190451025213501 ) ) ;
#121871=DIRECTION ( 'NONE',  ( -0.7071067811865486830, -0.7071067811865464625, 0.000000000000000000 ) ) ;
#121872=DIRECTION ( 'NONE',  ( -0.6830127018922181881, 0.6830127018922202975, -0.2588190451025214056 ) ) ;
#121873=VERTEX_POINT ( 'NONE', #82128 ) ;
#121874=EDGE_LOOP ( 'NONE', ( #21868, #78006, #2656, #117226 ) ) ;
#121875=EDGE_LOOP ( 'NONE', ( #36997, #4272, #33254, #3397 ) ) ;
#121876=DIRECTION ( 'NONE',  ( -0.7071067811865487940, 0.7071067811865463515, 0.000000000000000000 ) ) ;
#121877=LINE ( 'NONE', #21871, #109210 ) ;
#121879=VERTEX_POINT ( 'NONE', #37155 ) ;
#121881=PLANE ( 'NONE',  #138268 ) ;
#121882=EDGE_CURVE ( 'NONE', #83429, #54589, #60364, .T. ) ;
#121883=EDGE_CURVE ( 'NONE', #142433, #67739, #25552, .T. ) ;
#121884=LINE ( 'NONE', #142946, #13895 ) ;
#121885=EDGE_LOOP ( 'NONE', ( #82754, #94552, #12242, #122399 ) ) ;
#121886=CARTESIAN_POINT ( 'NONE',  ( 29.67183060077626067, -6.740707523384216415, 4.000000000000000000 ) ) ;
#121887=EDGE_CURVE ( 'NONE', #32567, #56766, #124162, .T. ) ;
#121888=DIRECTION ( 'NONE',  ( -0.7071067811865487940, 0.7071067811865463515, 0.000000000000000000 ) ) ;
#121890=VECTOR ( 'NONE', #114423, 1000.000000000000000 ) ;
#121891=CARTESIAN_POINT ( 'NONE',  ( -15.00548008471250228, 28.92564299267927552, 4.000000000000000000 ) ) ;
#121892=ORIENTED_EDGE ( 'NONE', *, *, #114002, .T. ) ;
#121894=DIRECTION ( 'NONE',  ( -0.000000000000000000, 1.000000000000000000, -0.000000000000000000 ) ) ;
#121895=CARTESIAN_POINT ( 'NONE',  ( -26.99451991528749417, 28.92564299267956685, 4.000000000000000000 ) ) ;
#121897=PLANE ( 'NONE',  #93514 ) ;
#121898=VERTEX_POINT ( 'NONE', #59648 ) ;
#121899=AXIS2_PLACEMENT_3D ( 'NONE', #55887, #101495, #737 ) ;
#121900=CARTESIAN_POINT ( 'NONE',  ( 27.18398860626900060, 28.73617430169806042, 5.000000000000000000 ) ) ;
#121901=VERTEX_POINT ( 'NONE', #3765 ) ;
#121902=PLANE ( 'NONE',  #14976 ) ;
#121903=DIRECTION ( 'NONE',  ( -0.000000000000000000, 0.3543493200069153248, 0.9351131265310292928 ) ) ;
#121906=ORIENTED_EDGE ( 'NONE', *, *, #59400, .F. ) ;
#121907=DIRECTION ( 'NONE',  ( -0.000000000000000000, 0.3543493200069153248, 0.9351131265310292928 ) ) ;
#121908=PLANE ( 'NONE',  #116229 ) ;
#121909=EDGE_CURVE ( 'NONE', #114745, #30259, #5211, .T. ) ;
#121910=VECTOR ( 'NONE', #87039, 1000.000000000000000 ) ;
#121911=ORIENTED_EDGE ( 'NONE', *, *, #10607, .F. ) ;
#121912=DIRECTION ( 'NONE',  ( -0.3543493200069162685, -0.000000000000000000, -0.9351131265310288487 ) ) ;
#121913=FACE_OUTER_BOUND ( 'NONE', #25171, .T. ) ;
#121914=ORIENTED_EDGE ( 'NONE', *, *, #97854, .T. ) ;
#121915=DIRECTION ( 'NONE',  ( 0.7071067811865487940, -0.7071067811865463515, 0.000000000000000000 ) ) ;
#121916=VECTOR ( 'NONE', #139193, 1000.000000000000227 ) ;
#121918=ORIENTED_EDGE ( 'NONE', *, *, #134703, .T. ) ;
#121919=EDGE_LOOP ( 'NONE', ( #50024, #29013, #114629, #122733 ) ) ;
#121920=PLANE ( 'NONE',  #142191 ) ;
#121921=PLANE ( 'NONE',  #133892 ) ;
#121922=ORIENTED_EDGE ( 'NONE', *, *, #85117, .T. ) ;
#121923=ADVANCED_FACE ( 'NONE', ( #69824 ), #126302, .F. ) ;
#121926=DIRECTION ( 'NONE',  ( 0.000000000000000000, -1.000000000000000000, 0.000000000000000000 ) ) ;
#121927=CARTESIAN_POINT ( 'NONE',  ( -12.29974487139158512, -27.71228299555214747, 4.000000000000000000 ) ) ;
#121928=VECTOR ( 'NONE', #107592, 1000.000000000000227 ) ;
#121929=VERTEX_POINT ( 'NONE', #82821 ) ;
#121931=EDGE_CURVE ( 'NONE', #140411, #72185, #58972, .T. ) ;
#121932=CARTESIAN_POINT ( 'NONE',  ( -20.81601139373100295, 28.73617430169773002, 5.000000000000000000 ) ) ;
#121933=AXIS2_PLACEMENT_3D ( 'NONE', #129274, #82941, #94503 ) ;
#121935=LINE ( 'NONE', #66876, #138603 ) ;
#121937=DIRECTION ( 'NONE',  ( 0.7071067811865487940, -0.7071067811865463515, 0.000000000000000000 ) ) ;
#121938=ORIENTED_EDGE ( 'NONE', *, *, #92964, .F. ) ;
#121939=ORIENTED_EDGE ( 'NONE', *, *, #43223, .T. ) ;
#121941=VERTEX_POINT ( 'NONE', #47378 ) ;
#121942=VECTOR ( 'NONE', #27912, 1000.000000000000000 ) ;
#121943=EDGE_CURVE ( 'NONE', #36373, #9222, #103125, .T. ) ;
#121944=ORIENTED_EDGE ( 'NONE', *, *, #60946, .F. ) ;
#121945=DIRECTION ( 'NONE',  ( -0.7071067811865486830, -0.7071067811865464625, 0.000000000000000000 ) ) ;
#121946=DIRECTION ( 'NONE',  ( -0.000000000000000000, 0.3543493200069153248, 0.9351131265310292928 ) ) ;
#121947=ORIENTED_EDGE ( 'NONE', *, *, #29455, .T. ) ;
#121948=DIRECTION ( 'NONE',  ( -0.6830127018922180770, -0.6830127018922204085, -0.2588190451025213501 ) ) ;
#121950=PLANE ( 'NONE',  #20899 ) ;
#121954=EDGE_CURVE ( 'NONE', #53059, #22625, #103804, .T. ) ;
#121955=VERTEX_POINT ( 'NONE', #102438 ) ;
#121956=DIRECTION ( 'NONE',  ( 0.7071067811865486830, -0.7071067811865464625, -0.000000000000000000 ) ) ;
#121957=CARTESIAN_POINT ( 'NONE',  ( 21.70710678118639692, -12.74070752338415247, 5.000000000000000000 ) ) ;
#121958=CARTESIAN_POINT ( 'NONE',  ( 0.000000000000000000, 0.000000000000000000, 5.000000000000000000 ) ) ;
#121960=FACE_OUTER_BOUND ( 'NONE', #107806, .T. ) ;
#121961=VECTOR ( 'NONE', #53005, 1000.000000000000000 ) ;
#121962=PLANE ( 'NONE',  #51583 ) ;
#121963=CARTESIAN_POINT ( 'NONE',  ( 7.828169399223478209, 3.759292476615683665, 4.000000000000000000 ) ) ;
#121964=VECTOR ( 'NONE', #79831, 1000.000000000000000 ) ;
#121966=CARTESIAN_POINT ( 'NONE',  ( 48.29974487139158867, -27.71228299555239971, 4.000000000000000000 ) ) ;
#121967=AXIS2_PLACEMENT_3D ( 'NONE', #116471, #127334, #86534 ) ;
#121968=FACE_OUTER_BOUND ( 'NONE', #39464, .T. ) ;
#121970=VERTEX_POINT ( 'NONE', #3089 ) ;
#121972=LINE ( 'NONE', #110379, #50928 ) ;
#121973=ADVANCED_FACE ( 'NONE', ( #136455 ), #79988, .F. ) ;
#121975=VECTOR ( 'NONE', #104531, 1000.000000000000000 ) ;
#121976=CARTESIAN_POINT ( 'NONE',  ( -21.71757738642552127, -21.73023691814493574, 5.000000000000000888 ) ) ;
#121977=VERTEX_POINT ( 'NONE', #15362 ) ;
#121979=DIRECTION ( 'NONE',  ( -0.6830127018922180770, -0.6830127018922204085, -0.2588190451025213501 ) ) ;
#121982=ORIENTED_EDGE ( 'NONE', *, *, #125143, .T. ) ;
#121984=VERTEX_POINT ( 'NONE', #71233 ) ;
#121985=VERTEX_POINT ( 'NONE', #49500 ) ;
#121986=PLANE ( 'NONE',  #95798 ) ;
#121989=ORIENTED_EDGE ( 'NONE', *, *, #18444, .F. ) ;
#121990=EDGE_CURVE ( 'NONE', #55621, #60957, #27694, .T. ) ;
#121991=DIRECTION ( 'NONE',  ( -0.7071067811865486830, -0.7071067811865464625, 0.000000000000000000 ) ) ;
#121994=EDGE_CURVE ( 'NONE', #57179, #124741, #38585, .T. ) ;
#121996=LINE ( 'NONE', #1626, #112577 ) ;
#121998=AXIS2_PLACEMENT_3D ( 'NONE', #99973, #91264, #26690 ) ;
#121999=CARTESIAN_POINT ( 'NONE',  ( 57.18398860626899705, 28.73617430169827358, 5.000000000000000000 ) ) ;
#122000=DIRECTION ( 'NONE',  ( -0.3543493200069163795, -9.265275131829747941E-33, -0.9351131265310288487 ) ) ;
#122001=ORIENTED_EDGE ( 'NONE', *, *, #113496, .F. ) ;
#122002=VECTOR ( 'NONE', #47454, 1000.000000000000000 ) ;
#122003=DIRECTION ( 'NONE',  ( 0.6830127018922180770, -0.6830127018922204085, -0.2588190451025213501 ) ) ;
#122005=CARTESIAN_POINT ( 'NONE',  ( -12.00548008471251293, 28.92564299267929684, 4.000000000000000000 ) ) ;
#122006=DIRECTION ( 'NONE',  ( -0.7071067811865487940, 0.7071067811865463515, -0.000000000000000000 ) ) ;
#122007=DIRECTION ( 'NONE',  ( -0.000000000000000000, 0.000000000000000000, 1.000000000000000000 ) ) ;
#122008=ORIENTED_EDGE ( 'NONE', *, *, #132007, .F. ) ;
#122010=CARTESIAN_POINT ( 'NONE',  ( -31.49999999999977973, -13.53360074219760101, 5.000000000000000000 ) ) ;
#122012=EDGE_LOOP ( 'NONE', ( #27908, #20219, #29558, #105588 ) ) ;
#122013=EDGE_CURVE ( 'NONE', #79902, #108305, #135078, .T. ) ;
#122015=VERTEX_POINT ( 'NONE', #91545 ) ;
#122016=DIRECTION ( 'NONE',  ( -0.3543493200069162685, -0.000000000000000000, -0.9351131265310288487 ) ) ;
#122017=FACE_OUTER_BOUND ( 'NONE', #14582, .T. ) ;
#122018=VECTOR ( 'NONE', #33412, 1000.000000000000000 ) ;
#122019=DIRECTION ( 'NONE',  ( -0.000000000000000000, 0.000000000000000000, 1.000000000000000000 ) ) ;
#122020=LINE ( 'NONE', #22686, #48843 ) ;
#122021=FACE_BOUND ( 'NONE', #21776, .T. ) ;
#122022=DIRECTION ( 'NONE',  ( -0.7071067811865486830, -0.7071067811865464625, -0.000000000000000000 ) ) ;
#122024=CARTESIAN_POINT ( 'NONE',  ( 6.707106781186499056, -15.74070752338412049, 5.000000000000000000 ) ) ;
#122025=LINE ( 'NONE', #112605, #110651 ) ;
#122026=ORIENTED_EDGE ( 'NONE', *, *, #120157, .F. ) ;
#122027=LINE ( 'NONE', #11838, #62629 ) ;
#122028=ORIENTED_EDGE ( 'NONE', *, *, #38510, .F. ) ;
#122029=EDGE_CURVE ( 'NONE', #54275, #67480, #69091, .T. ) ;
#122030=EDGE_CURVE ( 'NONE', #66308, #117459, #135761, .T. ) ;
#122031=VERTEX_POINT ( 'NONE', #8748 ) ;
#122033=ORIENTED_EDGE ( 'NONE', *, *, #59892, .F. ) ;
#122034=LINE ( 'NONE', #109751, #43059 ) ;
#122036=LINE ( 'NONE', #8956, #109140 ) ;
#122037=EDGE_CURVE ( 'NONE', #65337, #61284, #77142, .T. ) ;
#122038=ORIENTED_EDGE ( 'NONE', *, *, #604, .F. ) ;
#122039=FACE_OUTER_BOUND ( 'NONE', #8241, .T. ) ;
#122041=EDGE_CURVE ( 'NONE', #4252, #9940, #138623, .T. ) ;
#122042=LINE ( 'NONE', #35808, #123680 ) ;
#122044=PLANE ( 'NONE',  #124331 ) ;
#122045=DIRECTION ( 'NONE',  ( -0.000000000000000000, 0.000000000000000000, 1.000000000000000000 ) ) ;
#122046=DIRECTION ( 'NONE',  ( 0.7071067811865487940, 0.7071067811865463515, -0.000000000000000000 ) ) ;
#122047=DIRECTION ( 'NONE',  ( 0.6830127018922180770, -0.6830127018922204085, -0.2588190451025213501 ) ) ;
#122048=LINE ( 'NONE', #135807, #111811 ) ;
#122049=DIRECTION ( 'NONE',  ( 0.6830127018922181881, 0.6830127018922202975, -0.2588190451025214056 ) ) ;
#122050=ORIENTED_EDGE ( 'NONE', *, *, #108444, .T. ) ;
#122051=CARTESIAN_POINT ( 'NONE',  ( 0.000000000000000000, 0.000000000000000000, 5.000000000000000000 ) ) ;
#122052=VERTEX_POINT ( 'NONE', #63233 ) ;
#122053=LINE ( 'NONE', #88024, #128284 ) ;
#122055=ORIENTED_EDGE ( 'NONE', *, *, #85026, .F. ) ;
#122056=ORIENTED_EDGE ( 'NONE', *, *, #30756, .T. ) ;
#122057=AXIS2_PLACEMENT_3D ( 'NONE', #57887, #15715, #4840 ) ;
#122058=EDGE_LOOP ( 'NONE', ( #33312, #15235, #81615 ) ) ;
#122060=ADVANCED_FACE ( 'NONE', ( #30575 ), #61785, .T. ) ;
#122062=EDGE_LOOP ( 'NONE', ( #87906, #76241, #100036 ) ) ;
#122063=DIRECTION ( 'NONE',  ( 0.000000000000000000, 1.000000000000000000, -0.000000000000000000 ) ) ;
#122064=VECTOR ( 'NONE', #94559, 1000.000000000000000 ) ;
#122065=AXIS2_PLACEMENT_3D ( 'NONE', #57180, #102806, #57893 ) ;
#122067=CARTESIAN_POINT ( 'NONE',  ( 8.994519915287490619, 28.92564299267944250, 4.000000000000000000 ) ) ;
#122068=VECTOR ( 'NONE', #81200, 1000.000000000000000 ) ;
#122070=CARTESIAN_POINT ( 'NONE',  ( -59.99451991528749772, 28.92564299267980132, 4.000000000000000000 ) ) ;
#122071=ADVANCED_FACE ( 'NONE', ( #20371 ), #140732, .F. ) ;
#122072=ORIENTED_EDGE ( 'NONE', *, *, #48887, .T. ) ;
#122073=CARTESIAN_POINT ( 'NONE',  ( -45.48921356237309510, -27.52281430457087197, 5.000000000000000000 ) ) ;
#122074=CARTESIAN_POINT ( 'NONE',  ( 6.489213562373093325, -27.52281430457059841, 5.000000000000000000 ) ) ;
#122076=CARTESIAN_POINT ( 'NONE',  ( -24.00548008471250938, 28.92564299267921513, 4.000000000000000000 ) ) ;
#122077=EDGE_CURVE ( 'NONE', #9912, #60822, #130613, .T. ) ;
#122078=DIRECTION ( 'NONE',  ( -0.000000000000000000, 0.000000000000000000, 1.000000000000000000 ) ) ;
#122079=VERTEX_POINT ( 'NONE', #51618 ) ;
#122080=EDGE_LOOP ( 'NONE', ( #123017, #89425, #110080, #127098, #26569 ) ) ;
#122081=CARTESIAN_POINT ( 'NONE',  ( -8.018447346356650129, 18.75929247661552424, 20.33588619593444591 ) ) ;
#122082=CARTESIAN_POINT ( 'NONE',  ( 25.00193056682080339, -22.22500000000000142, 4.500000000000000888 ) ) ;
#122083=DIRECTION ( 'NONE',  ( 0.6830127018922181881, 0.6830127018922202975, -0.2588190451025214056 ) ) ;
#122084=VERTEX_POINT ( 'NONE', #107399 ) ;
#122085=CARTESIAN_POINT ( 'NONE',  ( 48.48921356237309510, -27.52281430457089328, 5.000000000000000000 ) ) ;
#122087=EDGE_LOOP ( 'NONE', ( #106176, #124108, #30416, #57898 ) ) ;
#122089=CARTESIAN_POINT ( 'NONE',  ( 23.99999999999984013, -10.44781430457072346, 5.000000000000000000 ) ) ;
#122090=LINE ( 'NONE', #78609, #31065 ) ;
#122091=ADVANCED_FACE ( 'NONE', ( #95810 ), #40734, .F. ) ;
#122092=CARTESIAN_POINT ( 'NONE',  ( 66.48921356237309510, -27.52281430457101763, 5.000000000000000000 ) ) ;
#122093=CARTESIAN_POINT ( 'NONE',  ( 34.17183060077623935, 3.759292476615688550, 4.000000000000000000 ) ) ;
#122094=CARTESIAN_POINT ( 'NONE',  ( -51.18398860626899705, 28.73617430169823095, 5.000000000000000000 ) ) ;
#122095=LINE ( 'NONE', #54039, #51742 ) ;
#122096=LINE ( 'NONE', #56194, #85370 ) ;
#122097=ORIENTED_EDGE ( 'NONE', *, *, #1162, .T. ) ;
#122098=CARTESIAN_POINT ( 'NONE',  ( 5.510786437626906675, -27.52281430457051314, 5.000000000000000000 ) ) ;
#122101=VECTOR ( 'NONE', #125090, 1000.000000000000000 ) ;
#122102=EDGE_CURVE ( 'NONE', #89832, #121130, #84940, .T. ) ;
#122103=DIRECTION ( 'NONE',  ( -0.7071067811865486830, 0.7071067811865464625, 0.000000000000000000 ) ) ;
#122104=CARTESIAN_POINT ( 'NONE',  ( -13.36246187583893530, 22.22500000000000142, 4.000000000000000000 ) ) ;
#122105=EDGE_CURVE ( 'NONE', #68584, #8173, #85636, .T. ) ;
#122107=VECTOR ( 'NONE', #134077, 1000.000000000000000 ) ;
#122108=EDGE_LOOP ( 'NONE', ( #85029, #9319, #55782, #72611 ) ) ;
#122109=PLANE ( 'NONE',  #99368 ) ;
#122110=FACE_OUTER_BOUND ( 'NONE', #137767, .T. ) ;
#122114=LINE ( 'NONE', #22769, #76662 ) ;
#122115=LINE ( 'NONE', #90954, #7592 ) ;
#122116=VECTOR ( 'NONE', #9858, 1000.000000000000000 ) ;
#122118=DIRECTION ( 'NONE',  ( 0.7071067811865487940, 0.7071067811865463515, 0.000000000000000000 ) ) ;
#122120=DIRECTION ( 'NONE',  ( -0.7071067811865486830, -0.7071067811865464625, 0.000000000000000000 ) ) ;
#122123=CARTESIAN_POINT ( 'NONE',  ( -27.00548008471251293, 28.92564299267919381, 4.000000000000000000 ) ) ;
#122124=ORIENTED_EDGE ( 'NONE', *, *, #29776, .T. ) ;
#122125=CARTESIAN_POINT ( 'NONE',  ( -5.218373117075014278, 21.74787736706806385, 4.999607392498049308 ) ) ;
#122126=VERTEX_POINT ( 'NONE', #18216 ) ;
#122127=CARTESIAN_POINT ( 'NONE',  ( 8.994519915287490619, 28.92564299267944250, 4.000000000000000000 ) ) ;
#122128=CARTESIAN_POINT ( 'NONE',  ( -33.18398860626899705, 28.73617430169810305, 5.000000000000000000 ) ) ;
#122129=FACE_OUTER_BOUND ( 'NONE', #50981, .T. ) ;
#122130=CARTESIAN_POINT ( 'NONE',  ( 11.99999999999992006, 2.342191155542461267, -5.001666872980111478 ) ) ;
#122131=LINE ( 'NONE', #90226, #120318 ) ;
#122132=CARTESIAN_POINT ( 'NONE',  ( -17.20003122016825614, 8.259292476615641476, 16.85664084051845180 ) ) ;
#122134=ORIENTED_EDGE ( 'NONE', *, *, #32894, .T. ) ;
#122137=CARTESIAN_POINT ( 'NONE',  ( -22.49999999999984013, -20.53675388469232388, 2.352720554255840923 ) ) ;
#122138=LINE ( 'NONE', #121435, #15634 ) ;
#122140=PLANE ( 'NONE',  #30064 ) ;
#122141=LINE ( 'NONE', #56243, #15875 ) ;
#122142=VERTEX_POINT ( 'NONE', #72694 ) ;
#122145=PLANE ( 'NONE',  #79436 ) ;
#122146=CARTESIAN_POINT ( 'NONE',  ( 32.99451991528749062, 28.92564299267960948, 4.000000000000000000 ) ) ;
#122147=PLANE ( 'NONE',  #10414 ) ;
#122148=ORIENTED_EDGE ( 'NONE', *, *, #37619, .F. ) ;
#122149=DIRECTION ( 'NONE',  ( -0.6830127018922181881, 0.6830127018922202975, -0.2588190451025214056 ) ) ;
#122150=VERTEX_POINT ( 'NONE', #129875 ) ;
#122151=VECTOR ( 'NONE', #135890, 1000.000000000000227 ) ;
#122152=DIRECTION ( 'NONE',  ( 1.000000000000000000, 0.000000000000000000, 0.000000000000000000 ) ) ;
#122154=ORIENTED_EDGE ( 'NONE', *, *, #66100, .T. ) ;
#122156=CARTESIAN_POINT ( 'NONE',  ( -34.49999999999976552, 0.05432934483094037370, 4.994342998332168548 ) ) ;
#122158=VECTOR ( 'NONE', #22869, 1000.000000000000000 ) ;
#122159=DIRECTION ( 'NONE',  ( 0.7071067811865487940, 0.7071067811865463515, 0.000000000000000000 ) ) ;
#122160=ADVANCED_FACE ( 'NONE', ( #74813 ), #19676, .F. ) ;
#122161=FACE_OUTER_BOUND ( 'NONE', #14917, .T. ) ;
#122164=EDGE_CURVE ( 'NONE', #92198, #109138, #135857, .T. ) ;
#122166=LINE ( 'NONE', #77295, #56933 ) ;
#122167=FACE_OUTER_BOUND ( 'NONE', #134194, .T. ) ;
#122169=DIRECTION ( 'NONE',  ( 0.7071067811865486830, -0.7071067811865464625, -0.000000000000000000 ) ) ;
#122170=VECTOR ( 'NONE', #23999, 1000.000000000000000 ) ;
#122171=ORIENTED_EDGE ( 'NONE', *, *, #26982, .T. ) ;
#122174=ORIENTED_EDGE ( 'NONE', *, *, #83308, .T. ) ;
#122175=ADVANCED_FACE ( 'NONE', ( #29829 ), #74071, .F. ) ;
#122176=CARTESIAN_POINT ( 'NONE',  ( -23.99999999999983302, 14.87792677143806230, -11.06722581663445482 ) ) ;
#122177=LINE ( 'NONE', #91024, #118199 ) ;
#122179=CARTESIAN_POINT ( 'NONE',  ( 0.000000000000000000, 0.000000000000000000, 5.000000000000000000 ) ) ;
#122181=ORIENTED_EDGE ( 'NONE', *, *, #67665, .T. ) ;
#122183=CARTESIAN_POINT ( 'NONE',  ( -25.82816939922334498, -8.240707523384196875, 4.000000000000000000 ) ) ;
#122185=EDGE_CURVE ( 'NONE', #61991, #130861, #42890, .T. ) ;
#122186=ORIENTED_EDGE ( 'NONE', *, *, #60650, .F. ) ;
#122187=DIRECTION ( 'NONE',  ( 0.6830127018922180770, -0.6830127018922204085, -0.2588190451025213501 ) ) ;
#122188=DIRECTION ( 'NONE',  ( -0.6830127018922180770, -0.6830127018922204085, -0.2588190451025213501 ) ) ;
#122189=DIRECTION ( 'NONE',  ( -0.6830127018922180770, -0.6830127018922204085, -0.2588190451025213501 ) ) ;
#122190=EDGE_CURVE ( 'NONE', #33921, #82671, #99352, .T. ) ;
#122192=FACE_BOUND ( 'NONE', #53793, .T. ) ;
#122193=CARTESIAN_POINT ( 'NONE',  ( -29.99999999999978328, -12.03360074219761700, 5.000000000000000000 ) ) ;
#122194=LINE ( 'NONE', #22867, #132335 ) ;
#122195=DIRECTION ( 'NONE',  ( -0.000000000000000000, 0.000000000000000000, 1.000000000000000000 ) ) ;
#122196=AXIS2_PLACEMENT_3D ( 'NONE', #93549, #92821, #37758 ) ;
#122197=EDGE_CURVE ( 'NONE', #88988, #121666, #81038, .T. ) ;
#122198=EDGE_CURVE ( 'NONE', #119727, #127658, #77654, .T. ) ;
#122199=DIRECTION ( 'NONE',  ( -0.3543493200069162685, -0.000000000000000000, -0.9351131265310288487 ) ) ;
#122200=CARTESIAN_POINT ( 'NONE',  ( 27.29974487139158512, -27.71228299555225405, 4.000000000000000000 ) ) ;
#122202=ORIENTED_EDGE ( 'NONE', *, *, #119565, .T. ) ;
#122203=ORIENTED_EDGE ( 'NONE', *, *, #115130, .F. ) ;
#122205=VERTEX_POINT ( 'NONE', #32722 ) ;
#122207=ORIENTED_EDGE ( 'NONE', *, *, #127816, .F. ) ;
#122208=ADVANCED_FACE ( 'NONE', ( #69452 ), #120375, .F. ) ;
#122209=LINE ( 'NONE', #43968, #102579 ) ;
#122210=CARTESIAN_POINT ( 'NONE',  ( 6.770042794577893375, 21.73644205237997440, 5.000000000000000888 ) ) ;
#122211=EDGE_CURVE ( 'NONE', #74950, #106339, #47518, .T. ) ;
#122213=CARTESIAN_POINT ( 'NONE',  ( -6.183988606268994381, 28.73617430169791476, 5.000000000000000000 ) ) ;
#122217=FACE_OUTER_BOUND ( 'NONE', #4464, .T. ) ;
#122218=DIRECTION ( 'NONE',  ( 1.000000000000000000, 0.000000000000000000, 0.000000000000000000 ) ) ;
#122219=FACE_OUTER_BOUND ( 'NONE', #109549, .T. ) ;
#122223=EDGE_CURVE ( 'NONE', #3283, #52621, #21823, .T. ) ;
#122224=LINE ( 'NONE', #102654, #112043 ) ;
#122226=VECTOR ( 'NONE', #100502, 1000.000000000000000 ) ;
#122227=EDGE_LOOP ( 'NONE', ( #71210, #41616, #63584, #49615 ) ) ;
#122228=VERTEX_POINT ( 'NONE', #76211 ) ;
#122229=EDGE_CURVE ( 'NONE', #58779, #105272, #125239, .T. ) ;
#122230=EDGE_CURVE ( 'NONE', #74252, #83338, #110229, .T. ) ;
#122231=ORIENTED_EDGE ( 'NONE', *, *, #122884, .F. ) ;
#122234=DIRECTION ( 'NONE',  ( -0.6830127018922180770, -0.6830127018922204085, -0.2588190451025213501 ) ) ;
#122236=VECTOR ( 'NONE', #67, 1000.000000000000000 ) ;
#122238=FACE_OUTER_BOUND ( 'NONE', #79807, .T. ) ;
#122239=EDGE_CURVE ( 'NONE', #30215, #140739, #25930, .T. ) ;
#122240=ORIENTED_EDGE ( 'NONE', *, *, #103395, .T. ) ;
#122241=LINE ( 'NONE', #88947, #60423 ) ;
#122242=EDGE_CURVE ( 'NONE', #91297, #56327, #36790, .T. ) ;
#122243=FACE_OUTER_BOUND ( 'NONE', #29826, .T. ) ;
#122244=ORIENTED_EDGE ( 'NONE', *, *, #112141, .T. ) ;
#122245=CARTESIAN_POINT ( 'NONE',  ( -2.510786437626908008, -27.52281430457053446, 5.000000000000000000 ) ) ;
#122246=CARTESIAN_POINT ( 'NONE',  ( 12.48921356237309155, -27.52281430457064104, 5.000000000000000000 ) ) ;
#122247=ORIENTED_EDGE ( 'NONE', *, *, #35835, .F. ) ;
#122250=ORIENTED_EDGE ( 'NONE', *, *, #23566, .F. ) ;
#122251=VERTEX_POINT ( 'NONE', #66764 ) ;
#122253=AXIS2_PLACEMENT_3D ( 'NONE', #5649, #29553, #139792 ) ;
#122254=DIRECTION ( 'NONE',  ( -0.7071067811865487940, 0.7071067811865463515, 0.000000000000000000 ) ) ;
#122256=LINE ( 'NONE', #22929, #78708 ) ;
#122257=LINE ( 'NONE', #67195, #106682 ) ;
#122258=ORIENTED_EDGE ( 'NONE', *, *, #84777, .T. ) ;
#122259=AXIS2_PLACEMENT_3D ( 'NONE', #139748, #107778, #77857 ) ;
#122262=EDGE_CURVE ( 'NONE', #88988, #122835, #10910, .T. ) ;
#122264=DIRECTION ( 'NONE',  ( 1.000000000000000000, 0.000000000000000000, 0.000000000000000000 ) ) ;
#122265=LINE ( 'NONE', #133884, #71475 ) ;
#122267=ORIENTED_EDGE ( 'NONE', *, *, #35191, .T. ) ;
#122268=ORIENTED_EDGE ( 'NONE', *, *, #19864, .T. ) ;
#122269=ORIENTED_EDGE ( 'NONE', *, *, #128352, .F. ) ;
#122270=PLANE ( 'NONE',  #76495 ) ;
#122271=DIRECTION ( 'NONE',  ( 0.3543493200069162685, -0.000000000000000000, -0.9351131265310288487 ) ) ;
#122274=DIRECTION ( 'NONE',  ( 0.7071067811865487940, 0.7071067811865463515, 0.000000000000000000 ) ) ;
#122275=DIRECTION ( 'NONE',  ( -0.000000000000000000, -0.3543493200069152693, 0.9351131265310292928 ) ) ;
#122276=DIRECTION ( 'NONE',  ( 0.7071067811865487940, 0.7071067811865463515, 0.000000000000000000 ) ) ;
#122277=DIRECTION ( 'NONE',  ( -0.000000000000000000, -0.000000000000000000, 1.000000000000000000 ) ) ;
#122278=DIRECTION ( 'NONE',  ( 1.000000000000000000, 0.000000000000000000, 0.000000000000000000 ) ) ;
#122279=DIRECTION ( 'NONE',  ( -0.7071067811865487940, 0.7071067811865463515, 0.000000000000000000 ) ) ;
#122281=CARTESIAN_POINT ( 'NONE',  ( 23.99451991528749062, 28.92564299267954908, 4.000000000000000000 ) ) ;
#122285=ORIENTED_EDGE ( 'NONE', *, *, #94998, .T. ) ;
#122286=VECTOR ( 'NONE', #90947, 1000.000000000000227 ) ;
#122287=VECTOR ( 'NONE', #75375, 1000.000000000000000 ) ;
#122288=CARTESIAN_POINT ( 'NONE',  ( 25.49999999999981526, -10.53360074219763121, 5.000000000000000000 ) ) ;
#122290=ORIENTED_EDGE ( 'NONE', *, *, #4519, .F. ) ;
#122291=DIRECTION ( 'NONE',  ( 1.000000000000000000, 0.000000000000000000, 0.000000000000000000 ) ) ;
#122292=DIRECTION ( 'NONE',  ( -0.6830127018922180770, -0.6830127018922204085, -0.2588190451025213501 ) ) ;
#122293=VERTEX_POINT ( 'NONE', #132765 ) ;
#122295=VERTEX_POINT ( 'NONE', #33453 ) ;
#122296=LINE ( 'NONE', #44817, #104664 ) ;
#122297=VERTEX_POINT ( 'NONE', #89229 ) ;
#122298=FACE_OUTER_BOUND ( 'NONE', #11877, .T. ) ;
#122301=LINE ( 'NONE', #22974, #101819 ) ;
#122302=DIRECTION ( 'NONE',  ( 0.3543493200069162685, -0.000000000000000000, -0.9351131265310288487 ) ) ;
#122303=DIRECTION ( 'NONE',  ( 0.7071067811865487940, 0.7071067811865463515, 0.000000000000000000 ) ) ;
#122306=AXIS2_PLACEMENT_3D ( 'NONE', #96358, #107261, #107948 ) ;
#122307=CARTESIAN_POINT ( 'NONE',  ( -34.92500000000001137, 3.759292476615678336, 4.255531930566252008 ) ) ;
#122308=CARTESIAN_POINT ( 'NONE',  ( -51.18398860626899705, 28.73617430169823095, 5.000000000000000000 ) ) ;
#122309=ORIENTED_EDGE ( 'NONE', *, *, #36454, .F. ) ;
#122310=VECTOR ( 'NONE', #114949, 1000.000000000000000 ) ;
#122311=EDGE_LOOP ( 'NONE', ( #32351, #62120, #100611, #128490, #87151, #58891 ) ) ;
#122315=DIRECTION ( 'NONE',  ( -0.7071067811865486830, 0.7071067811865464625, 0.000000000000000000 ) ) ;
#122316=DIRECTION ( 'NONE',  ( 0.000000000000000000, 1.000000000000000000, 0.000000000000000000 ) ) ;
#122317=DIRECTION ( 'NONE',  ( -0.7071067811865486830, 0.7071067811865464625, 0.000000000000000000 ) ) ;
#122318=LINE ( 'NONE', #35377, #112672 ) ;
#122319=EDGE_LOOP ( 'NONE', ( #121099, #43183, #32368, #123940 ) ) ;
#122320=LINE ( 'NONE', #57129, #52113 ) ;
#122322=EDGE_CURVE ( 'NONE', #114028, #84504, #34140, .T. ) ;
#122323=LINE ( 'NONE', #36078, #129837 ) ;
#122324=CARTESIAN_POINT ( 'NONE',  ( 0.7700427945779364514, 21.73644205237998150, 5.000000000000000888 ) ) ;
#122326=EDGE_CURVE ( 'NONE', #121813, #46067, #103462, .T. ) ;
#122327=CARTESIAN_POINT ( 'NONE',  ( 20.51078643762690490, -27.52281430457041012, 5.000000000000000000 ) ) ;
#122328=CARTESIAN_POINT ( 'NONE',  ( -34.92500000000001137, 22.22500000000000142, 4.000000000000000000 ) ) ;
#122329=ORIENTED_EDGE ( 'NONE', *, *, #48426, .F. ) ;
#122330=DIRECTION ( 'NONE',  ( -0.7071067811865486830, -0.7071067811865464625, -0.000000000000000000 ) ) ;
#122331=CARTESIAN_POINT ( 'NONE',  ( 21.00548008471250938, 28.92564299267923644, 4.000000000000000000 ) ) ;
#122332=LINE ( 'NONE', #101319, #3012 ) ;
#122334=DIRECTION ( 'NONE',  ( -0.3543493200069162685, -0.000000000000000000, -0.9351131265310288487 ) ) ;
#122335=EDGE_CURVE ( 'NONE', #135502, #98260, #115034, .T. ) ;
#122337=VERTEX_POINT ( 'NONE', #116502 ) ;
#122338=ORIENTED_EDGE ( 'NONE', *, *, #73508, .F. ) ;
#122339=ORIENTED_EDGE ( 'NONE', *, *, #142876, .T. ) ;
#122342=EDGE_CURVE ( 'NONE', #71721, #42777, #84600, .T. ) ;
#122343=CARTESIAN_POINT ( 'NONE',  ( -36.48921356237310221, -27.52281430457080802, 5.000000000000000000 ) ) ;
#122344=DIRECTION ( 'NONE',  ( 0.7071067811865487940, 0.7071067811865463515, -0.000000000000000000 ) ) ;
#122347=VERTEX_POINT ( 'NONE', #93321 ) ;
#122348=CARTESIAN_POINT ( 'NONE',  ( 39.48921356237310221, -27.52281430457082934, 5.000000000000000000 ) ) ;
#122349=CARTESIAN_POINT ( 'NONE',  ( -32.99999999999976552, -9.412538124160658271, 4.000000000000000000 ) ) ;
#122350=EDGE_CURVE ( 'NONE', #126030, #118230, #94717, .T. ) ;
#122351=CARTESIAN_POINT ( 'NONE',  ( 5.816011393731002066, 28.73617430169783304, 5.000000000000000000 ) ) ;
#122353=ORIENTED_EDGE ( 'NONE', *, *, #12008, .F. ) ;
#122354=VECTOR ( 'NONE', #57415, 1000.000000000000227 ) ;
#122355=LINE ( 'NONE', #55715, #48948 ) ;
#122357=VECTOR ( 'NONE', #14179, 1000.000000000000227 ) ;
#122359=AXIS2_PLACEMENT_3D ( 'NONE', #126719, #115826, #74527 ) ;
#122360=VECTOR ( 'NONE', #138637, 1000.000000000000000 ) ;
#122361=VERTEX_POINT ( 'NONE', #59306 ) ;
#122363=AXIS2_PLACEMENT_3D ( 'NONE', #38083, #126483, #115575 ) ;
#122364=DIRECTION ( 'NONE',  ( -0.7071067811865486830, -0.7071067811865464625, -0.000000000000000000 ) ) ;
#122365=AXIS2_PLACEMENT_3D ( 'NONE', #55628, #99088, #75944 ) ;
#122367=DIRECTION ( 'NONE',  ( -0.000000000000000000, 0.000000000000000000, 1.000000000000000000 ) ) ;
#122368=ADVANCED_FACE ( 'NONE', ( #82457 ), #4828, .T. ) ;
#122370=VECTOR ( 'NONE', #40830, 999.9999999999998863 ) ;
#122372=CARTESIAN_POINT ( 'NONE',  ( 72.18398860626899705, 28.73617430169837661, 5.000000000000000000 ) ) ;
#122373=DIRECTION ( 'NONE',  ( -0.7071067811865486830, -0.7071067811865464625, 0.000000000000000000 ) ) ;
#122374=EDGE_LOOP ( 'NONE', ( #18043, #128653, #30076, #119139 ) ) ;
#122376=CARTESIAN_POINT ( 'NONE',  ( -36.18398860626899705, 28.73617430169812437, 5.000000000000000000 ) ) ;
#122377=ORIENTED_EDGE ( 'NONE', *, *, #31678, .F. ) ;
#122378=VERTEX_POINT ( 'NONE', #61452 ) ;
#122381=( BOUNDED_CURVE ( )  B_SPLINE_CURVE ( 3, ( #113321, #80736, #2404, #90901 ),
 .UNSPECIFIED., .F., .F. ) 
 B_SPLINE_CURVE_WITH_KNOTS ( ( 4, 4 ),
 ( 5.043186909253408956, 5.074607125596330093 ),
 .UNSPECIFIED. ) 
 CURVE ( )  GEOMETRIC_REPRESENTATION_ITEM ( )  RATIONAL_B_SPLINE_CURVE ( ( 1.000000000000000000, 0.9999177325257868620, 0.9999177325257868620, 1.000000000000000000 ) ) 
 REPRESENTATION_ITEM ( '' )  );
#122382=ADVANCED_FACE ( 'NONE', ( #48385 ), #60743, .F. ) ;
#122384=CARTESIAN_POINT ( 'NONE',  ( -29.99999999999979039, 16.93112307739200872, 4.000000000000000000 ) ) ;
#122385=ORIENTED_EDGE ( 'NONE', *, *, #137726, .T. ) ;
#122386=LINE ( 'NONE', #67332, #71474 ) ;
#122387=CARTESIAN_POINT ( 'NONE',  ( -65.99451991528749772, 28.92564299267984396, 4.000000000000000000 ) ) ;
#122388=ADVANCED_FACE ( 'NONE', ( #27329 ), #71578, .F. ) ;
#122389=LINE ( 'NONE', #130449, #33990 ) ;
#122392=AXIS2_PLACEMENT_3D ( 'NONE', #54462, #25902, #99335 ) ;
#122393=( BOUNDED_CURVE ( )  B_SPLINE_CURVE ( 3, ( #16543, #81866, #106385, #93417 ),
 .UNSPECIFIED., .F., .T. ) 
 B_SPLINE_CURVE_WITH_KNOTS ( ( 4, 4 ),
 ( 5.106027341939283204, 6.645403452391245303 ),
 .UNSPECIFIED. ) 
 CURVE ( )  GEOMETRIC_REPRESENTATION_ITEM ( )  RATIONAL_B_SPLINE_CURVE ( ( 1.000000000000000000, 0.8120851936182283959, 0.8120851936182283959, 1.000000000000000000 ) ) 
 REPRESENTATION_ITEM ( '' )  );
#122394=ORIENTED_EDGE ( 'NONE', *, *, #74947, .F. ) ;
#122395=VECTOR ( 'NONE', #39618, 1000.000000000000000 ) ;
#122396=EDGE_CURVE ( 'NONE', #65645, #106882, #28067, .T. ) ;
#122397=DIRECTION ( 'NONE',  ( -0.7071067811865486830, -0.7071067811865464625, -0.000000000000000000 ) ) ;
#122399=ORIENTED_EDGE ( 'NONE', *, *, #133470, .F. ) ;
#122400=DIRECTION ( 'NONE',  ( -0.7071067811865486830, 0.7071067811865464625, 0.000000000000000000 ) ) ;
#122401=VERTEX_POINT ( 'NONE', #139714 ) ;
#122402=LINE ( 'NONE', #78946, #79365 ) ;
#122403=VERTEX_POINT ( 'NONE', #16441 ) ;
#122404=PLANE ( 'NONE',  #138546 ) ;
#122405=ORIENTED_EDGE ( 'NONE', *, *, #57438, .T. ) ;
#122406=ORIENTED_EDGE ( 'NONE', *, *, #101607, .T. ) ;
#122407=VECTOR ( 'NONE', #48158, 1000.000000000000000 ) ;
#122408=VERTEX_POINT ( 'NONE', #29474 ) ;
#122409=VECTOR ( 'NONE', #44924, 1000.000000000000000 ) ;
#122410=DIRECTION ( 'NONE',  ( -0.000000000000000000, 0.000000000000000000, 1.000000000000000000 ) ) ;
#122411=CARTESIAN_POINT ( 'NONE',  ( 17.99451991528748351, 28.92564299267950645, 4.000000000000000000 ) ) ;
#122413=FACE_OUTER_BOUND ( 'NONE', #26624, .T. ) ;
#122415=DIRECTION ( 'NONE',  ( 0.7071067811865487940, 0.7071067811865463515, 0.000000000000000000 ) ) ;
#122417=VECTOR ( 'NONE', #70784, 1000.000000000000000 ) ;
#122418=ADVANCED_FACE ( 'NONE', ( #42541 ), #65000, .F. ) ;
#122419=DIRECTION ( 'NONE',  ( -0.7071067811865487940, 0.7071067811865463515, 0.000000000000000000 ) ) ;
#122420=LINE ( 'NONE', #46346, #101508 ) ;
#122421=ORIENTED_EDGE ( 'NONE', *, *, #142931, .T. ) ;
#122422=DIRECTION ( 'NONE',  ( 1.000000000000000000, 0.000000000000000000, 0.000000000000000000 ) ) ;
#122423=CARTESIAN_POINT ( 'NONE',  ( -26.67183060077628198, -6.740707523384214639, 4.000000000000000000 ) ) ;
#122424=FACE_OUTER_BOUND ( 'NONE', #29941, .T. ) ;
#122425=ORIENTED_EDGE ( 'NONE', *, *, #18474, .T. ) ;
#122427=ORIENTED_EDGE ( 'NONE', *, *, #132577, .T. ) ;
#122428=DIRECTION ( 'NONE',  ( -0.3543493200069162685, -0.000000000000000000, -0.9351131265310288487 ) ) ;
#122429=VERTEX_POINT ( 'NONE', #64267 ) ;
#122430=ORIENTED_EDGE ( 'NONE', *, *, #48938, .F. ) ;
#122433=CARTESIAN_POINT ( 'NONE',  ( 78.18398860626899705, 28.73617430169841924, 5.000000000000000000 ) ) ;
#122434=EDGE_CURVE ( 'NONE', #96838, #61667, #141844, .T. ) ;
#122435=DIRECTION ( 'NONE',  ( -0.000000000000000000, 0.3543493200069153248, 0.9351131265310292928 ) ) ;
#122436=CARTESIAN_POINT ( 'NONE',  ( -11.57672154193639003, 11.25929247661560240, 17.85071094206587361 ) ) ;
#122437=EDGE_LOOP ( 'NONE', ( #39845, #64605, #96224, #27356 ) ) ;
#122439=ORIENTED_EDGE ( 'NONE', *, *, #54470, .F. ) ;
#122440=CARTESIAN_POINT ( 'NONE',  ( -53.99451991528749062, 28.92564299267975869, 4.000000000000000000 ) ) ;
#122441=EDGE_CURVE ( 'NONE', #77873, #141023, #130253, .T. ) ;
#122443=VERTEX_POINT ( 'NONE', #118634 ) ;
#122445=CARTESIAN_POINT ( 'NONE',  ( -3.707106781186512823, -0.7407075233842770334, 5.000000000000000000 ) ) ;
#122447=ORIENTED_EDGE ( 'NONE', *, *, #110579, .F. ) ;
#122448=VERTEX_POINT ( 'NONE', #86744 ) ;
#122449=ORIENTED_EDGE ( 'NONE', *, *, #42272, .F. ) ;
#122450=LINE ( 'NONE', #55810, #75069 ) ;
#122451=CARTESIAN_POINT ( 'NONE',  ( 32.99451991528749062, 28.92564299267960948, 4.000000000000000000 ) ) ;
#122452=CARTESIAN_POINT ( 'NONE',  ( 34.92499999999998295, -1.298069433179003695, 4.500000000000000888 ) ) ;
#122453=LINE ( 'NONE', #108700, #140032 ) ;
#122454=DIRECTION ( 'NONE',  ( 0.6830127018922180770, -0.6830127018922204085, -0.2588190451025213501 ) ) ;
#122455=ORIENTED_EDGE ( 'NONE', *, *, #80007, .T. ) ;
#122459=LINE ( 'NONE', #142803, #60803 ) ;
#122460=ORIENTED_EDGE ( 'NONE', *, *, #95661, .T. ) ;
#122463=VECTOR ( 'NONE', #47628, 1000.000000000000227 ) ;
#122464=VECTOR ( 'NONE', #14126, 1000.000000000000227 ) ;
#122466=ORIENTED_EDGE ( 'NONE', *, *, #17599, .F. ) ;
#122467=CARTESIAN_POINT ( 'NONE',  ( -29.67183060077626067, 17.25929247661553845, 4.000000000000000000 ) ) ;
#122468=ORIENTED_EDGE ( 'NONE', *, *, #12357, .T. ) ;
#122469=ORIENTED_EDGE ( 'NONE', *, *, #13274, .T. ) ;
#122470=EDGE_CURVE ( 'NONE', #28997, #75489, #143249, .T. ) ;
#122471=DIRECTION ( 'NONE',  ( 0.7071067811865486830, -0.7071067811865464625, -0.000000000000000000 ) ) ;
#122472=DIRECTION ( 'NONE',  ( 0.7071067811865486830, -0.7071067811865464625, -0.000000000000000000 ) ) ;
#122473=ORIENTED_EDGE ( 'NONE', *, *, #40898, .T. ) ;
#122474=DIRECTION ( 'NONE',  ( 0.7071067811865487940, 0.7071067811865463515, 0.000000000000000000 ) ) ;
#122475=CARTESIAN_POINT ( 'NONE',  ( 15.48921356237309510, -27.52281430457066236, 5.000000000000000000 ) ) ;
#122477=LINE ( 'NONE', #78291, #117893 ) ;
#122479=LINE ( 'NONE', #111630, #76702 ) ;
#122480=LINE ( 'NONE', #21765, #5138 ) ;
#122481=CARTESIAN_POINT ( 'NONE',  ( 33.79289321881321939, 15.75929247661555976, 5.000000000000000000 ) ) ;
#122482=CARTESIAN_POINT ( 'NONE',  ( 30.18398860626900060, 28.73617430169808173, 5.000000000000000000 ) ) ;
#122484=DIRECTION ( 'NONE',  ( 0.7071067811865486830, -0.7071067811865464625, -0.000000000000000000 ) ) ;
#122485=AXIS2_PLACEMENT_3D ( 'NONE', #137668, #115858, #49242 ) ;
#122486=PLANE ( 'NONE',  #138568 ) ;
#122488=DIRECTION ( 'NONE',  ( 0.7071067811865487940, -0.7071067811865463515, 0.000000000000000000 ) ) ;
#122489=LINE ( 'NONE', #31933, #6055 ) ;
#122491=ORIENTED_EDGE ( 'NONE', *, *, #116592, .T. ) ;
#122493=AXIS2_PLACEMENT_3D ( 'NONE', #123458, #56058, #22639 ) ;
#122494=VERTEX_POINT ( 'NONE', #117878 ) ;
#122495=VERTEX_POINT ( 'NONE', #18580 ) ;
#122496=VERTEX_POINT ( 'NONE', #99011 ) ;
#122497=DIRECTION ( 'NONE',  ( 0.7071067811865486830, -0.7071067811865464625, -0.000000000000000000 ) ) ;
#122498=DIRECTION ( 'NONE',  ( 0.6830127018922181881, 0.6830127018922202975, -0.2588190451025214056 ) ) ;
#122500=VERTEX_POINT ( 'NONE', #8404 ) ;
#122501=AXIS2_PLACEMENT_3D ( 'NONE', #50513, #94698, #128091 ) ;
#122502=FACE_OUTER_BOUND ( 'NONE', #69917, .T. ) ;
#122506=AXIS2_PLACEMENT_3D ( 'NONE', #62071, #29407, #41724 ) ;
#122507=CARTESIAN_POINT ( 'NONE',  ( -17.11087965568911073, 8.820243421702873121, 4.000000000000000000 ) ) ;
#122508=CARTESIAN_POINT ( 'NONE',  ( -51.48921356237309510, -27.52281430457091460, 5.000000000000000000 ) ) ;
#122509=EDGE_LOOP ( 'NONE', ( #66072, #112770, #91092, #139062 ) ) ;
#122512=DIRECTION ( 'NONE',  ( 0.7071067811865487940, -0.7071067811865463515, 0.000000000000000000 ) ) ;
#122513=DIRECTION ( 'NONE',  ( -0.000000000000000000, 0.000000000000000000, 1.000000000000000000 ) ) ;
#122514=VECTOR ( 'NONE', #59260, 1000.000000000000000 ) ;
#122516=CARTESIAN_POINT ( 'NONE',  ( 42.18398860626899705, 28.73617430169816700, 5.000000000000000000 ) ) ;
#122517=CARTESIAN_POINT ( 'NONE',  ( -18.18398860626898994, 28.73617430169800002, 5.000000000000000000 ) ) ;
#122518=VECTOR ( 'NONE', #32056, 999.9999999999998863 ) ;
#122521=ADVANCED_FACE ( 'NONE', ( #141087 ), #41079, .F. ) ;
#122522=EDGE_CURVE ( 'NONE', #25072, #93715, #51971, .T. ) ;
#122523=EDGE_LOOP ( 'NONE', ( #45448, #36001, #5877, #74403 ) ) ;
#122524=ORIENTED_EDGE ( 'NONE', *, *, #52236, .F. ) ;
#122526=EDGE_CURVE ( 'NONE', #130061, #140080, #10567, .T. ) ;
#122527=VERTEX_POINT ( 'NONE', #41801 ) ;
#122528=EDGE_CURVE ( 'NONE', #123836, #50567, #120770, .T. ) ;
#122529=DIRECTION ( 'NONE',  ( -0.7071067811865487940, 0.7071067811865463515, 0.000000000000000000 ) ) ;
#122530=EDGE_CURVE ( 'NONE', #58012, #41530, #43241, .T. ) ;
#122532=CARTESIAN_POINT ( 'NONE',  ( 0.000000000000000000, 4.931123077392136622, 4.000000000000000000 ) ) ;
#122534=ADVANCED_FACE ( 'NONE', ( #75172 ), #20019, .T. ) ;
#122536=ORIENTED_EDGE ( 'NONE', *, *, #50931, .T. ) ;
#122537=ORIENTED_EDGE ( 'NONE', *, *, #53861, .F. ) ;
#122538=CARTESIAN_POINT ( 'NONE',  ( 0.2997448713915885632, -27.71228299555206220, 4.000000000000000000 ) ) ;
#122540=EDGE_CURVE ( 'NONE', #74817, #88053, #53380, .T. ) ;
#122542=ORIENTED_EDGE ( 'NONE', *, *, #52776, .F. ) ;
#122544=EDGE_LOOP ( 'NONE', ( #42098, #55199, #117189, #20380 ) ) ;
#122546=EDGE_CURVE ( 'NONE', #87653, #121, #98332, .T. ) ;
#122548=ORIENTED_EDGE ( 'NONE', *, *, #92956, .F. ) ;
#122549=DIRECTION ( 'NONE',  ( -0.7071067811865486830, -0.7071067811865464625, -0.000000000000000000 ) ) ;
#122550=ORIENTED_EDGE ( 'NONE', *, *, #30309, .F. ) ;
#122551=ORIENTED_EDGE ( 'NONE', *, *, #119597, .T. ) ;
#122552=ORIENTED_EDGE ( 'NONE', *, *, #42389, .T. ) ;
#122553=ADVANCED_FACE ( 'NONE', ( #58439 ), #78711, .F. ) ;
#122555=LINE ( 'NONE', #34875, #48830 ) ;
#122556=EDGE_LOOP ( 'NONE', ( #129189, #102435, #128278, #123503 ) ) ;
#122557=LINE ( 'NONE', #67516, #115400 ) ;
#122558=EDGE_CURVE ( 'NONE', #117128, #13716, #80165, .T. ) ;
#122559=AXIS2_PLACEMENT_3D ( 'NONE', #105602, #138265, #139722 ) ;
#122560=DIRECTION ( 'NONE',  ( -0.7071067811865486830, -0.7071067811865464625, 0.000000000000000000 ) ) ;
#122562=VECTOR ( 'NONE', #135818, 999.9999999999998863 ) ;
#122563=AXIS2_PLACEMENT_3D ( 'NONE', #44614, #135862, #78629 ) ;
#122564=AXIS2_PLACEMENT_3D ( 'NONE', #120452, #30656, #42251 ) ;
#122565=ADVANCED_FACE ( 'NONE', ( #23607 ), #22159, .F. ) ;
#122566=CARTESIAN_POINT ( 'NONE',  ( -30.48921356237309510, -27.52281430457076894, 5.000000000000000000 ) ) ;
#122568=FACE_BOUND ( 'NONE', #108518, .T. ) ;
#122569=EDGE_LOOP ( 'NONE', ( #89255, #55807, #9762, #87627 ) ) ;
#122570=CARTESIAN_POINT ( 'NONE',  ( -15.08491323193753075, -12.74070752338414891, 18.74364270924350606 ) ) ;
#122571=CARTESIAN_POINT ( 'NONE',  ( -26.99999999999981171, -21.03360074219752462, 5.000000000000000000 ) ) ;
#122573=CARTESIAN_POINT ( 'NONE',  ( -12.48921356237309155, -27.52281430457064104, 5.000000000000000000 ) ) ;
#122575=DIRECTION ( 'NONE',  ( -0.000000000000000000, 0.000000000000000000, 1.000000000000000000 ) ) ;
#122576=ORIENTED_EDGE ( 'NONE', *, *, #64594, .T. ) ;
#122578=VECTOR ( 'NONE', #112344, 1000.000000000000000 ) ;
#122579=EDGE_CURVE ( 'NONE', #77421, #100584, #91039, .T. ) ;
#122580=EDGE_LOOP ( 'NONE', ( #35028, #21164, #75658, #16851 ) ) ;
#122582=ORIENTED_EDGE ( 'NONE', *, *, #16201, .F. ) ;
#122584=PLANE ( 'NONE',  #67259 ) ;
#122585=FACE_OUTER_BOUND ( 'NONE', #52210, .T. ) ;
#122586=EDGE_CURVE ( 'NONE', #28861, #126820, #91907, .T. ) ;
#122587=ORIENTED_EDGE ( 'NONE', *, *, #66644, .F. ) ;
#122588=LINE ( 'NONE', #110274, #12080 ) ;
#122589=PLANE ( 'NONE',  #48140 ) ;
#122591=VECTOR ( 'NONE', #20395, 1000.000000000000000 ) ;
#122592=VECTOR ( 'NONE', #72308, 1000.000000000000000 ) ;
#122594=DIRECTION ( 'NONE',  ( -0.3543493200069162685, -0.000000000000000000, -0.9351131265310288487 ) ) ;
#122595=CARTESIAN_POINT ( 'NONE',  ( -36.29974487139159578, -27.71228299555231445, 4.000000000000000000 ) ) ;
#122596=EDGE_CURVE ( 'NONE', #4187, #78485, #1121, .T. ) ;
#122597=LINE ( 'NONE', #13815, #7680 ) ;
#122598=ORIENTED_EDGE ( 'NONE', *, *, #65967, .F. ) ;
#122599=ORIENTED_EDGE ( 'NONE', *, *, #26163, .T. ) ;
#122600=ORIENTED_EDGE ( 'NONE', *, *, #28466, .T. ) ;
#122601=ORIENTED_EDGE ( 'NONE', *, *, #41684, .T. ) ;
#122603=CARTESIAN_POINT ( 'NONE',  ( 16.49999999999988987, -4.533600742197687161, 5.000000000000000000 ) ) ;
#122604=LINE ( 'NONE', #109595, #430 ) ;
#122605=ORIENTED_EDGE ( 'NONE', *, *, #10947, .F. ) ;
#122606=VECTOR ( 'NONE', #31404, 1000.000000000000000 ) ;
#122608=EDGE_LOOP ( 'NONE', ( #4264, #54504, #99961, #100037 ) ) ;
#122610=CARTESIAN_POINT ( 'NONE',  ( 31.49999999999978684, -19.53360074219753884, 5.000000000000000000 ) ) ;
#122611=EDGE_CURVE ( 'NONE', #81705, #50033, #67124, .T. ) ;
#122612=CARTESIAN_POINT ( 'NONE',  ( -34.92500000000001137, 22.22500000000000142, 4.000000000000000000 ) ) ;
#122613=EDGE_LOOP ( 'NONE', ( #63892, #57117, #128900, #131732 ) ) ;
#122614=AXIS2_PLACEMENT_3D ( 'NONE', #80125, #1076, #24284 ) ;
#122615=CARTESIAN_POINT ( 'NONE',  ( -63.48921356237309510, -27.52281430457099631, 5.000000000000000000 ) ) ;
#122616=FACE_OUTER_BOUND ( 'NONE', #16707, .T. ) ;
#122617=EDGE_CURVE ( 'NONE', #100722, #131560, #79478, .T. ) ;
#122619=DIRECTION ( 'NONE',  ( 0.7071067811865486830, -0.7071067811865464625, -0.000000000000000000 ) ) ;
#122620=ORIENTED_EDGE ( 'NONE', *, *, #83255, .T. ) ;
#122622=CARTESIAN_POINT ( 'NONE',  ( 30.18398860626900060, 28.73617430169808173, 5.000000000000000000 ) ) ;
#122623=LINE ( 'NONE', #58138, #18769 ) ;
#122624=DIRECTION ( 'NONE',  ( 0.3543493200069162685, -0.000000000000000000, -0.9351131265310288487 ) ) ;
#122625=DIRECTION ( 'NONE',  ( 0.7071067811865486830, -0.7071067811865464625, -0.000000000000000000 ) ) ;
#122627=CARTESIAN_POINT ( 'NONE',  ( -8.671830600776411657, 14.25929247661557220, 4.000000000000000000 ) ) ;
#122628=ORIENTED_EDGE ( 'NONE', *, *, #37304, .T. ) ;
#122629=LINE ( 'NONE', #79901, #27682 ) ;
#122630=VERTEX_POINT ( 'NONE', #123670 ) ;
#122631=LINE ( 'NONE', #121202, #82188 ) ;
#122632=DIRECTION ( 'NONE',  ( -0.000000000000000000, 0.000000000000000000, 1.000000000000000000 ) ) ;
#122633=LINE ( 'NONE', #2254, #95796 ) ;
#122635=EDGE_CURVE ( 'NONE', #39039, #90401, #110591, .T. ) ;
#122636=CARTESIAN_POINT ( 'NONE',  ( 0.000000000000000000, 0.000000000000000000, 5.000000000000000000 ) ) ;
#122639=DIRECTION ( 'NONE',  ( -0.000000000000000000, 0.3543493200069153248, 0.9351131265310292928 ) ) ;
#122640=DIRECTION ( 'NONE',  ( -0.000000000000000000, 0.3543493200069153248, 0.9351131265310292928 ) ) ;
#122641=EDGE_LOOP ( 'NONE', ( #62292, #109858, #36976, #55022 ) ) ;
#122642=LINE ( 'NONE', #111785, #107124 ) ;
#122643=ORIENTED_EDGE ( 'NONE', *, *, #111613, .T. ) ;
#122644=LINE ( 'NONE', #45837, #71637 ) ;
#122645=DIRECTION ( 'NONE',  ( 0.7071067811865487940, 0.7071067811865463515, 0.000000000000000000 ) ) ;
#122646=ORIENTED_EDGE ( 'NONE', *, *, #118800, .T. ) ;
#122647=EDGE_CURVE ( 'NONE', #49545, #70705, #69276, .T. ) ;
#122648=ORIENTED_EDGE ( 'NONE', *, *, #140154, .F. ) ;
#122651=EDGE_LOOP ( 'NONE', ( #79428, #11520, #23848, #7991 ) ) ;
#122652=CARTESIAN_POINT ( 'NONE',  ( 21.00548008471250938, 28.92564299267923644, 4.000000000000000000 ) ) ;
#122653=LINE ( 'NONE', #105878, #29859 ) ;
#122656=CARTESIAN_POINT ( 'NONE',  ( 31.82816939922330235, 15.75929247661555799, 4.000000000000000000 ) ) ;
#122657=CARTESIAN_POINT ( 'NONE',  ( 39.48921356237310221, -27.52281430457082934, 5.000000000000000000 ) ) ;
#122659=DIRECTION ( 'NONE',  ( 0.6830127018922181881, 0.6830127018922202975, -0.2588190451025214056 ) ) ;
#122661=CARTESIAN_POINT ( 'NONE',  ( -5.999999999999955591, 16.55218569542900298, 5.000000000000000000 ) ) ;
#122663=EDGE_LOOP ( 'NONE', ( #135981, #36677, #87241, #16182, #8235, #142732 ) ) ;
#122664=DIRECTION ( 'NONE',  ( -0.7071067811865487940, 0.7071067811865463515, -0.000000000000000000 ) ) ;
#122665=AXIS2_PLACEMENT_3D ( 'NONE', #80935, #24392, #59208 ) ;
#122666=ORIENTED_EDGE ( 'NONE', *, *, #135362, .F. ) ;
#122667=ORIENTED_EDGE ( 'NONE', *, *, #107653, .F. ) ;
#122668=ORIENTED_EDGE ( 'NONE', *, *, #8599, .F. ) ;
#122670=LINE ( 'NONE', #69776, #115729 ) ;
#122671=VECTOR ( 'NONE', #79881, 1000.000000000000000 ) ;
#122672=AXIS2_PLACEMENT_3D ( 'NONE', #114936, #104073, #4729 ) ;
#122674=VERTEX_POINT ( 'NONE', #89575 ) ;
#122675=LINE ( 'NONE', #90797, #67062 ) ;
#122676=CARTESIAN_POINT ( 'NONE',  ( 18.48921356237309510, -27.52281430457068367, 5.000000000000000000 ) ) ;
#122678=CARTESIAN_POINT ( 'NONE',  ( 2.999999999999978240, -13.06887692260767864, 4.000000000000000000 ) ) ;
#122679=CARTESIAN_POINT ( 'NONE',  ( 0.005480084712502889671, 28.92564299267938210, 4.000000000000000000 ) ) ;
#122681=ORIENTED_EDGE ( 'NONE', *, *, #48962, .F. ) ;
#122682=CARTESIAN_POINT ( 'NONE',  ( -8.292893218813397027, 8.259292476615632594, 5.000000000000000000 ) ) ;
#122683=DIRECTION ( 'NONE',  ( -0.7071067811865487940, 0.7071067811865463515, 0.000000000000000000 ) ) ;
#122684=DIRECTION ( 'NONE',  ( -0.6830127018922180770, -0.6830127018922204085, -0.2588190451025213501 ) ) ;
#122687=DIRECTION ( 'NONE',  ( -0.7071067811865486830, -0.7071067811865464625, 0.000000000000000000 ) ) ;
#122688=LINE ( 'NONE', #11043, #65364 ) ;
#122689=CARTESIAN_POINT ( 'NONE',  ( 2.816011393730999401, 28.73617430169785436, 5.000000000000000000 ) ) ;
#122691=CARTESIAN_POINT ( 'NONE',  ( 22.49999999999984368, 11.52377502935405040, -1.522421517564136906 ) ) ;
#122693=CARTESIAN_POINT ( 'NONE',  ( -20.70822291016940397, -15.74070752338411694, 19.73771281079092788 ) ) ;
#122694=EDGE_LOOP ( 'NONE', ( #127145, #109717, #32646, #102699 ) ) ;
#122695=ORIENTED_EDGE ( 'NONE', *, *, #88593, .F. ) ;
#122697=ADVANCED_FACE ( 'NONE', ( #406 ), #88896, .F. ) ;
#122699=ADVANCED_FACE ( 'NONE', ( #34492 ), #80868, .T. ) ;
#122700=AXIS2_PLACEMENT_3D ( 'NONE', #121245, #141593, #96603 ) ;
#122701=VECTOR ( 'NONE', #141492, 1000.000000000000000 ) ;
#122702=CARTESIAN_POINT ( 'NONE',  ( -5.994519915287488843, 28.92564299267942118, 4.000000000000000000 ) ) ;
#122703=ORIENTED_EDGE ( 'NONE', *, *, #98152, .F. ) ;
#122707=VECTOR ( 'NONE', #122899, 1000.000000000000227 ) ;
#122709=ORIENTED_EDGE ( 'NONE', *, *, #70849, .F. ) ;
#122710=EDGE_CURVE ( 'NONE', #23067, #93995, #49680, .T. ) ;
#122711=VECTOR ( 'NONE', #95221, 1000.000000000000000 ) ;
#122712=CARTESIAN_POINT ( 'NONE',  ( 41.99451991528749062, 28.92564299267967343, 4.000000000000000000 ) ) ;
#122713=VERTEX_POINT ( 'NONE', #138816 ) ;
#122714=ORIENTED_EDGE ( 'NONE', *, *, #118983, .T. ) ;
#122716=VECTOR ( 'NONE', #117325, 1000.000000000000000 ) ;
#122717=CARTESIAN_POINT ( 'NONE',  ( 27.48921356237309155, -27.52281430457074762, 5.000000000000000000 ) ) ;
#122718=DIRECTION ( 'NONE',  ( 0.7071067811865487940, 0.7071067811865463515, 0.000000000000000000 ) ) ;
#122719=EDGE_CURVE ( 'NONE', #89577, #85868, #37354, .T. ) ;
#122721=ORIENTED_EDGE ( 'NONE', *, *, #5017, .T. ) ;
#122722=ADVANCED_FACE ( 'NONE', ( #81590 ), #39506, .T. ) ;
#122724=VERTEX_POINT ( 'NONE', #125057 ) ;
#122725=VECTOR ( 'NONE', #60231, 1000.000000000000000 ) ;
#122726=DIRECTION ( 'NONE',  ( -0.7071067811865486830, -0.7071067811865464625, 0.000000000000000000 ) ) ;
#122727=DIRECTION ( 'NONE',  ( -0.7071067811865487940, 0.7071067811865463515, -0.000000000000000000 ) ) ;
#122728=CARTESIAN_POINT ( 'NONE',  ( -9.489213562373095101, -27.52281430457062328, 5.000000000000000000 ) ) ;
#122731=DIRECTION ( 'NONE',  ( -0.7071067811865487940, 0.7071067811865463515, -0.000000000000000000 ) ) ;
#122733=ORIENTED_EDGE ( 'NONE', *, *, #18342, .F. ) ;
#122734=VECTOR ( 'NONE', #70730, 1000.000000000000000 ) ;
#122735=CARTESIAN_POINT ( 'NONE',  ( 0.09667064187405399744, -2.240707523384260824, 15.26439735382752616 ) ) ;
#122737=DIRECTION ( 'NONE',  ( -0.7071067811865486830, -0.7071067811865464625, -0.000000000000000000 ) ) ;
#122738=PLANE ( 'NONE',  #82563 ) ;
#122740=ORIENTED_EDGE ( 'NONE', *, *, #56358, .T. ) ;
#122741=AXIS2_PLACEMENT_3D ( 'NONE', #43005, #12488, #98775 ) ;
#122743=ORIENTED_EDGE ( 'NONE', *, *, #101040, .F. ) ;
#122745=ORIENTED_EDGE ( 'NONE', *, *, #67446, .T. ) ;
#122747=CARTESIAN_POINT ( 'NONE',  ( 24.48921356237309510, -27.52281430457072631, 5.000000000000000000 ) ) ;
#122749=DIRECTION ( 'NONE',  ( -0.7071067811865486830, 0.7071067811865464625, 0.000000000000000000 ) ) ;
#122750=VECTOR ( 'NONE', #51676, 1000.000000000000000 ) ;
#122751=DIRECTION ( 'NONE',  ( -0.7071067811865486830, 0.7071067811865464625, 0.000000000000000000 ) ) ;
#122752=FACE_BOUND ( 'NONE', #72538, .T. ) ;
#122753=CARTESIAN_POINT ( 'NONE',  ( -1.446650576632166452, 2.259292476615694323, 14.86850063742354777 ) ) ;
#122754=DIRECTION ( 'NONE',  ( 0.7071067811865487940, -0.7071067811865463515, 0.000000000000000000 ) ) ;
#122755=DIRECTION ( 'NONE',  ( -0.7071067811865486830, 0.7071067811865464625, 0.000000000000000000 ) ) ;
#122756=DIRECTION ( 'NONE',  ( 0.7071067811865486830, -0.7071067811865464625, -0.000000000000000000 ) ) ;
#122757=ORIENTED_EDGE ( 'NONE', *, *, #125500, .F. ) ;
#122758=VECTOR ( 'NONE', #54771, 1000.000000000000000 ) ;
#122760=EDGE_LOOP ( 'NONE', ( #134989, #119365, #38941, #105144 ) ) ;
#122761=EDGE_LOOP ( 'NONE', ( #71065, #81123, #130908, #139156 ) ) ;
#122763=ORIENTED_EDGE ( 'NONE', *, *, #109675, .T. ) ;
#122764=CARTESIAN_POINT ( 'NONE',  ( -8.510786437626906675, -27.52281430457049183, 5.000000000000000000 ) ) ;
#122765=DIRECTION ( 'NONE',  ( 0.000000000000000000, -1.000000000000000000, 0.000000000000000000 ) ) ;
#122766=ADVANCED_FACE ( 'NONE', ( #135937 ), #127195, .F. ) ;
#122767=ORIENTED_EDGE ( 'NONE', *, *, #61997, .F. ) ;
#122768=DIRECTION ( 'NONE',  ( -0.6830127018922180770, -0.6830127018922204085, -0.2588190451025213501 ) ) ;
#122769=AXIS2_PLACEMENT_3D ( 'NONE', #142634, #31730, #89671 ) ;
#122772=AXIS2_PLACEMENT_3D ( 'NONE', #47620, #80235, #90360 ) ;
#122773=CARTESIAN_POINT ( 'NONE',  ( 3.793339364578457662, 21.75929247661549937, 4.998822639870711626 ) ) ;
#122774=ADVANCED_FACE ( 'NONE', ( #25747 ), #59825, .T. ) ;
#122779=DIRECTION ( 'NONE',  ( 0.7071067811865487940, 0.7071067811865463515, 0.000000000000000000 ) ) ;
#122780=VECTOR ( 'NONE', #140734, 999.9999999999998863 ) ;
#122781=EDGE_LOOP ( 'NONE', ( #21521, #20408, #43881, #3596 ) ) ;
#122782=VECTOR ( 'NONE', #67775, 1000.000000000000000 ) ;
#122785=ORIENTED_EDGE ( 'NONE', *, *, #104489, .F. ) ;
#122786=AXIS2_PLACEMENT_3D ( 'NONE', #97194, #61777, #95081 ) ;
#122787=DIRECTION ( 'NONE',  ( 0.7071067811865487940, 0.7071067811865463515, -0.000000000000000000 ) ) ;
#122788=CARTESIAN_POINT ( 'NONE',  ( -8.816011393731004731, 28.73617430169781173, 5.000000000000000000 ) ) ;
#122789=ORIENTED_EDGE ( 'NONE', *, *, #98378, .T. ) ;
#122790=VECTOR ( 'NONE', #52019, 1000.000000000000000 ) ;
#122792=ORIENTED_EDGE ( 'NONE', *, *, #48739, .T. ) ;
#122793=EDGE_CURVE ( 'NONE', #131487, #122496, #114182, .T. ) ;
#122794=EDGE_CURVE ( 'NONE', #79126, #112433, #48952, .T. ) ;
#122796=ORIENTED_EDGE ( 'NONE', *, *, #1610, .T. ) ;
#122797=VECTOR ( 'NONE', #91136, 999.9999999999998863 ) ;
#122798=LINE ( 'NONE', #132282, #78787 ) ;
#122802=EDGE_LOOP ( 'NONE', ( #36678, #31198, #97630, #75360 ) ) ;
#122804=CARTESIAN_POINT ( 'NONE',  ( -31.78678096696621580, 12.75929247661558641, 10.29404684609028209 ) ) ;
#122806=CARTESIAN_POINT ( 'NONE',  ( -60.18398860626900415, 28.73617430169829490, 5.000000000000000000 ) ) ;
#122807=DIRECTION ( 'NONE',  ( 0.000000000000000000, -0.3543493200069152138, 0.9351131265310292928 ) ) ;
#122808=EDGE_LOOP ( 'NONE', ( #85462, #59196, #96604, #39051 ) ) ;
#122809=ORIENTED_EDGE ( 'NONE', *, *, #63226, .T. ) ;
#122810=DIRECTION ( 'NONE',  ( 0.3543493200069162685, -0.000000000000000000, -0.9351131265310288487 ) ) ;
#122811=CARTESIAN_POINT ( 'NONE',  ( -6.712309939660236147, -21.73547319004780576, 4.999917730833664642 ) ) ;
#122812=PLANE ( 'NONE',  #14677 ) ;
#122814=VECTOR ( 'NONE', #81052, 1000.000000000000227 ) ;
#122815=PLANE ( 'NONE',  #94428 ) ;
#122816=CARTESIAN_POINT ( 'NONE',  ( 21.48921356237309155, -27.52281430457070499, 5.000000000000000000 ) ) ;
#122817=VECTOR ( 'NONE', #4490, 1000.000000000000227 ) ;
#122818=ADVANCED_FACE ( 'NONE', ( #126475 ), #50370, .T. ) ;
#122819=ORIENTED_EDGE ( 'NONE', *, *, #7836, .F. ) ;
#122820=EDGE_CURVE ( 'NONE', #30495, #139670, #16261, .T. ) ;
#122821=VECTOR ( 'NONE', #102398, 1000.000000000000227 ) ;
#122822=LINE ( 'NONE', #27783, #125867 ) ;
#122823=CARTESIAN_POINT ( 'NONE',  ( 20.99999999999985789, 20.70535890316563155, 1.956823837851868086 ) ) ;
#122824=DIRECTION ( 'NONE',  ( 0.7071067811865486830, -0.7071067811865464625, -0.000000000000000000 ) ) ;
#122825=CARTESIAN_POINT ( 'NONE',  ( 1.499999999999992673, 1.466399257802244893, 5.000000000000000000 ) ) ;
#122826=AXIS2_PLACEMENT_3D ( 'NONE', #109103, #84534, #87377 ) ;
#122827=LINE ( 'NONE', #56893, #30839 ) ;
#122828=FACE_OUTER_BOUND ( 'NONE', #118439, .T. ) ;
#122829=LINE ( 'NONE', #135166, #141988 ) ;
#122830=EDGE_CURVE ( 'NONE', #48693, #61439, #83741, .T. ) ;
#122831=CARTESIAN_POINT ( 'NONE',  ( 28.49999999999980815, -5.947814304570768762, 5.000000000000000000 ) ) ;
#122834=EDGE_CURVE ( 'NONE', #88432, #47660, #19861, .T. ) ;
#122835=VERTEX_POINT ( 'NONE', #85833 ) ;
#122837=CARTESIAN_POINT ( 'NONE',  ( 4.190181675744454104, -18.74070752338408852, 7.910009926591497376 ) ) ;
#122839=FACE_OUTER_BOUND ( 'NONE', #81846, .T. ) ;
#122840=EDGE_LOOP ( 'NONE', ( #88044, #63746, #31719, #8211 ) ) ;
#122842=DIRECTION ( 'NONE',  ( -0.000000000000000000, 0.3543493200069153248, 0.9351131265310292928 ) ) ;
#122843=DIRECTION ( 'NONE',  ( -0.7071067811865486830, 0.7071067811865464625, 0.000000000000000000 ) ) ;
#122844=ORIENTED_EDGE ( 'NONE', *, *, #94771, .F. ) ;
#122845=DIRECTION ( 'NONE',  ( 0.7071067811865486830, -0.7071067811865464625, -0.000000000000000000 ) ) ;
#122846=PLANE ( 'NONE',  #118314 ) ;
#122847=AXIS2_PLACEMENT_3D ( 'NONE', #141233, #64399, #86877 ) ;
#122848=CARTESIAN_POINT ( 'NONE',  ( -0.005480084712502889671, 28.92564299267938210, 4.000000000000000000 ) ) ;
#122851=ADVANCED_FACE ( 'NONE', ( #109734 ), #29311, .F. ) ;
#122852=CARTESIAN_POINT ( 'NONE',  ( 6.489213562373093325, -27.52281430457059841, 5.000000000000000000 ) ) ;
#122853=CARTESIAN_POINT ( 'NONE',  ( -34.92500000000001137, -8.240707523384193323, 4.255531930566235133 ) ) ;
#122854=EDGE_LOOP ( 'NONE', ( #89776, #28520, #49110, #54283 ) ) ;
#122855=CARTESIAN_POINT ( 'NONE',  ( -22.17183060077631751, 9.759292476615618384, 4.000000000000000000 ) ) ;
#122857=VECTOR ( 'NONE', #55976, 1000.000000000000227 ) ;
#122860=CARTESIAN_POINT ( 'NONE',  ( 31.22674160717815184, -11.24070752338416490, 18.24660765846989818 ) ) ;
#122863=CARTESIAN_POINT ( 'NONE',  ( -28.82816939922331656, 0.7592924766157138627, 4.000000000000000000 ) ) ;
#122864=ORIENTED_EDGE ( 'NONE', *, *, #68244, .T. ) ;
#122865=VERTEX_POINT ( 'NONE', #117718 ) ;
#122866=DIRECTION ( 'NONE',  ( 0.7071067811865487940, -0.7071067811865463515, 0.000000000000000000 ) ) ;
#122868=AXIS2_PLACEMENT_3D ( 'NONE', #98777, #77078, #34261 ) ;
#122869=PLANE ( 'NONE',  #109861 ) ;
#122872=CARTESIAN_POINT ( 'NONE',  ( 22.82816939922338051, -20.24070752338406720, 4.000000000000000000 ) ) ;
#122873=EDGE_CURVE ( 'NONE', #36826, #97582, #73553, .T. ) ;
#122874=DIRECTION ( 'NONE',  ( -0.000000000000000000, 0.000000000000000000, 1.000000000000000000 ) ) ;
#122875=VERTEX_POINT ( 'NONE', #42366 ) ;
#122878=ADVANCED_FACE ( 'NONE', ( #40232 ), #52491, .F. ) ;
#122879=FACE_OUTER_BOUND ( 'NONE', #93775, .T. ) ;
#122880=PLANE ( 'NONE',  #42857 ) ;
#122882=VECTOR ( 'NONE', #142480, 1000.000000000000000 ) ;
#122883=EDGE_CURVE ( 'NONE', #87653, #104458, #43076, .T. ) ;
#122884=EDGE_CURVE ( 'NONE', #42638, #48700, #8934, .T. ) ;
#122885=CARTESIAN_POINT ( 'NONE',  ( 2.510786437626908008, -27.52281430457053446, 5.000000000000000000 ) ) ;
#122886=AXIS2_PLACEMENT_3D ( 'NONE', #115065, #27358, #127399 ) ;
#122887=VECTOR ( 'NONE', #27873, 1000.000000000000000 ) ;
#122890=EDGE_LOOP ( 'NONE', ( #63384, #40786, #73283, #86761 ) ) ;
#122891=VERTEX_POINT ( 'NONE', #65564 ) ;
#122892=VECTOR ( 'NONE', #51363, 1000.000000000000227 ) ;
#122893=VECTOR ( 'NONE', #84528, 1000.000000000000000 ) ;
#122894=CARTESIAN_POINT ( 'NONE',  ( -33.70679250724053588, 20.25929247661551358, 20.83292124670822432 ) ) ;
#122896=CARTESIAN_POINT ( 'NONE',  ( 27.71757738642548574, -21.73023691814493574, 5.000000000000000888 ) ) ;
#122899=DIRECTION ( 'NONE',  ( 0.3543493200069162685, -0.000000000000000000, -0.9351131265310288487 ) ) ;
#122900=EDGE_CURVE ( 'NONE', #22203, #110486, #75694, .T. ) ;
#122902=CARTESIAN_POINT ( 'NONE',  ( -5.999999999999956479, -15.03360074219758502, 5.000000000000000000 ) ) ;
#122903=VERTEX_POINT ( 'NONE', #98158 ) ;
#122906=DIRECTION ( 'NONE',  ( 0.7071067811865487940, -0.7071067811865463515, 0.000000000000000000 ) ) ;
#122907=VECTOR ( 'NONE', #115712, 1000.000000000000000 ) ;
#122908=DIRECTION ( 'NONE',  ( 0.7071067811865486830, -0.7071067811865464625, -0.000000000000000000 ) ) ;
#122909=ORIENTED_EDGE ( 'NONE', *, *, #58596, .T. ) ;
#122910=EDGE_CURVE ( 'NONE', #121970, #12022, #7547, .T. ) ;
#122913=VERTEX_POINT ( 'NONE', #21307 ) ;
#122915=CARTESIAN_POINT ( 'NONE',  ( 28.17183060077627843, -5.240707523384230626, 4.000000000000000000 ) ) ;
#122916=CARTESIAN_POINT ( 'NONE',  ( 27.77004279457773350, 21.73644205237998150, 5.000000000000000888 ) ) ;
#122918=VECTOR ( 'NONE', #112847, 999.9999999999998863 ) ;
#122919=CARTESIAN_POINT ( 'NONE',  ( 15.75860074219783513, 21.72499999999999432, 5.000000000000000000 ) ) ;
#122920=CARTESIAN_POINT ( 'NONE',  ( -34.45011844616455221, 4.516280811637433779, 5.000000000000000888 ) ) ;
#122921=ORIENTED_EDGE ( 'NONE', *, *, #120246, .T. ) ;
#122922=VERTEX_POINT ( 'NONE', #87278 ) ;
#122923=EDGE_CURVE ( 'NONE', #121049, #87976, #95992, .T. ) ;
#122924=DIRECTION ( 'NONE',  ( 1.000000000000000000, 0.000000000000000000, 0.000000000000000000 ) ) ;
#122926=VECTOR ( 'NONE', #18234, 999.9999999999998863 ) ;
#122927=ORIENTED_EDGE ( 'NONE', *, *, #104007, .F. ) ;
#122928=AXIS2_PLACEMENT_3D ( 'NONE', #12687, #1779, #35206 ) ;
#122929=LINE ( 'NONE', #35231, #104592 ) ;
#122930=DIRECTION ( 'NONE',  ( 0.7071067811865487940, 0.7071067811865463515, 0.000000000000000000 ) ) ;
#122931=EDGE_CURVE ( 'NONE', #13309, #60163, #40920, .T. ) ;
#122932=VECTOR ( 'NONE', #142143, 1000.000000000000000 ) ;
#122933=ORIENTED_EDGE ( 'NONE', *, *, #18009, .F. ) ;
#122934=FACE_BOUND ( 'NONE', #28735, .T. ) ;
#122936=DIRECTION ( 'NONE',  ( 0.7071067811865487940, 0.7071067811865463515, -0.000000000000000000 ) ) ;
#122937=ADVANCED_FACE ( 'NONE', ( #96678 ), #85124, .F. ) ;
#122938=DIRECTION ( 'NONE',  ( 0.6830127018922181881, 0.6830127018922202975, -0.2588190451025214056 ) ) ;
#122939=LINE ( 'NONE', #70728, #126911 ) ;
#122941=CARTESIAN_POINT ( 'NONE',  ( -20.28769006033958533, -21.73547319004782352, 4.999917730833664642 ) ) ;
#122943=ADVANCED_FACE ( 'NONE', ( #64095 ), #76415, .F. ) ;
#122944=EDGE_LOOP ( 'NONE', ( #63350, #123837, #33447, #121454 ) ) ;
#122945=VECTOR ( 'NONE', #51273, 999.9999999999998863 ) ;
#122946=ORIENTED_EDGE ( 'NONE', *, *, #110611, .F. ) ;
#122948=ORIENTED_EDGE ( 'NONE', *, *, #73135, .F. ) ;
#122949=LINE ( 'NONE', #23624, #111399 ) ;
#122950=ORIENTED_EDGE ( 'NONE', *, *, #123429, .F. ) ;
#122951=VECTOR ( 'NONE', #17838, 1000.000000000000227 ) ;
#122952=DIRECTION ( 'NONE',  ( 1.000000000000000000, 0.000000000000000000, 0.000000000000000000 ) ) ;
#122955=CARTESIAN_POINT ( 'NONE',  ( -34.92500000000001137, 19.44114312045508441, 6.054907437694472705 ) ) ;
#122956=ORIENTED_EDGE ( 'NONE', *, *, #80541, .T. ) ;
#122957=DIRECTION ( 'NONE',  ( 0.7071067811865487940, 0.7071067811865463515, 0.000000000000000000 ) ) ;
#122958=FACE_OUTER_BOUND ( 'NONE', #140706, .T. ) ;
#122960=CARTESIAN_POINT ( 'NONE',  ( -14.99999999999990230, -13.39766691384885000, -10.96608748226462282 ) ) ;
#122961=LINE ( 'NONE', #23641, #1013 ) ;
#122963=VECTOR ( 'NONE', #16340, 1000.000000000000000 ) ;
#122964=CARTESIAN_POINT ( 'NONE',  ( 2.510786437626908008, -27.52281430457053446, 5.000000000000000000 ) ) ;
#122965=ORIENTED_EDGE ( 'NONE', *, *, #27579, .F. ) ;
#122967=CARTESIAN_POINT ( 'NONE',  ( 20.26628700938065109, -22.22500000000000142, -15.91404180650398814 ) ) ;
#122968=ORIENTED_EDGE ( 'NONE', *, *, #100476, .F. ) ;
#122969=ORIENTED_EDGE ( 'NONE', *, *, #83350, .F. ) ;
#122970=EDGE_CURVE ( 'NONE', #74632, #90138, #89413, .T. ) ;
#122971=ORIENTED_EDGE ( 'NONE', *, *, #140154, .T. ) ;
#122973=VECTOR ( 'NONE', #7858, 999.9999999999998863 ) ;
#122975=CARTESIAN_POINT ( 'NONE',  ( 11.99999999999992006, 8.587461875839162317, 4.000000000000000000 ) ) ;
#122978=( BOUNDED_CURVE ( )  B_SPLINE_CURVE ( 3, ( #20897, #7875, #65161, #109351 ),
 .UNSPECIFIED., .F., .T. ) 
 B_SPLINE_CURVE_WITH_KNOTS ( ( 4, 4 ),
 ( 2.001653308786155883, 3.503810798801451742 ),
 .UNSPECIFIED. ) 
 CURVE ( )  GEOMETRIC_REPRESENTATION_ITEM ( )  RATIONAL_B_SPLINE_CURVE ( ( 1.000000000000000000, 0.8206354192515208368, 0.8206354192515208368, 1.000000000000000000 ) ) 
 REPRESENTATION_ITEM ( '' )  );
#122979=DIRECTION ( 'NONE',  ( -0.7071067811865486830, -0.7071067811865464625, 0.000000000000000000 ) ) ;
#122980=VERTEX_POINT ( 'NONE', #112597 ) ;
#122982=DIRECTION ( 'NONE',  ( -0.6830127018922180770, -0.6830127018922204085, -0.2588190451025213501 ) ) ;
#122984=CARTESIAN_POINT ( 'NONE',  ( -20.99999999999984723, 20.58746187583902909, 4.000000000000000000 ) ) ;
#122986=DIRECTION ( 'NONE',  ( -0.6830127018922180770, -0.6830127018922204085, -0.2588190451025213501 ) ) ;
#122988=VECTOR ( 'NONE', #4865, 1000.000000000000227 ) ;
#122989=DIRECTION ( 'NONE',  ( -0.3543493200069163240, 4.681814790819596721E-17, -0.9351131265310288487 ) ) ;
#122990=VECTOR ( 'NONE', #115752, 1000.000000000000000 ) ;
#122992=CARTESIAN_POINT ( 'NONE',  ( -81.48921356237309510, -27.52281430457112066, 5.000000000000000000 ) ) ;
#122993=ORIENTED_EDGE ( 'NONE', *, *, #12202, .T. ) ;
#122994=ORIENTED_EDGE ( 'NONE', *, *, #12647, .F. ) ;
#122995=ORIENTED_EDGE ( 'NONE', *, *, #95589, .F. ) ;
#122996=FACE_OUTER_BOUND ( 'NONE', #63549, .T. ) ;
#122998=VECTOR ( 'NONE', #77943, 1000.000000000000000 ) ;
#123000=VECTOR ( 'NONE', #100638, 999.9999999999998863 ) ;
#123002=LINE ( 'NONE', #112134, #128427 ) ;
#123003=EDGE_CURVE ( 'NONE', #53919, #43072, #78546, .T. ) ;
#123004=PLANE ( 'NONE',  #41763 ) ;
#123005=EDGE_CURVE ( 'NONE', #141849, #109521, #34319, .T. ) ;
#123006=FACE_OUTER_BOUND ( 'NONE', #12919, .T. ) ;
#123009=CARTESIAN_POINT ( 'NONE',  ( 34.49999999999975842, -15.29013452822851349, 0.3645803511611147019 ) ) ;
#123011=CARTESIAN_POINT ( 'NONE',  ( -18.32816939922340538, 20.25929247661551003, 4.000000000000000000 ) ) ;
#123012=PLANE ( 'NONE',  #59888 ) ;
#123013=EDGE_CURVE ( 'NONE', #120532, #117668, #121319, .T. ) ;
#123014=VECTOR ( 'NONE', #15210, 1000.000000000000000 ) ;
#123015=DIRECTION ( 'NONE',  ( -0.3543493200069163240, -0.000000000000000000, -0.9351131265310288487 ) ) ;
#123016=EDGE_LOOP ( 'NONE', ( #50731, #74303, #108500 ) ) ;
#123017=ORIENTED_EDGE ( 'NONE', *, *, #21883, .F. ) ;
#123018=EDGE_LOOP ( 'NONE', ( #25912, #53884, #62062, #120538 ) ) ;
#123019=CARTESIAN_POINT ( 'NONE',  ( 0.000000000000000000, 0.000000000000000000, 5.000000000000000000 ) ) ;
#123020=CARTESIAN_POINT ( 'NONE',  ( 9.489213562373095101, -27.52281430457062328, 5.000000000000000000 ) ) ;
#123021=FACE_OUTER_BOUND ( 'NONE', #53311, .T. ) ;
#123022=LINE ( 'NONE', #86830, #124666 ) ;
#123024=EDGE_CURVE ( 'NONE', #87648, #128406, #134362, .T. ) ;
#123026=VECTOR ( 'NONE', #12887, 999.9999999999998863 ) ;
#123027=CARTESIAN_POINT ( 'NONE',  ( 21.48921356237309155, -27.52281430457070499, 5.000000000000000000 ) ) ;
#123028=DIRECTION ( 'NONE',  ( 0.3543493200069162685, -0.000000000000000000, -0.9351131265310288487 ) ) ;
#123029=CARTESIAN_POINT ( 'NONE',  ( 34.42499999999998295, 0.000000000000000000, 4.500000000000000888 ) ) ;
#123030=VECTOR ( 'NONE', #54534, 1000.000000000000227 ) ;
#123032=DIRECTION ( 'NONE',  ( 0.000000000000000000, -1.000000000000000000, 0.000000000000000000 ) ) ;
#123033=VERTEX_POINT ( 'NONE', #101710 ) ;
#123034=EDGE_CURVE ( 'NONE', #123294, #2398, #54663, .T. ) ;
#123037=ORIENTED_EDGE ( 'NONE', *, *, #105580, .T. ) ;
#123039=DIRECTION ( 'NONE',  ( 1.000000000000000000, 0.000000000000000000, 0.000000000000000000 ) ) ;
#123040=VERTEX_POINT ( 'NONE', #1648 ) ;
#123041=AXIS2_PLACEMENT_3D ( 'NONE', #120483, #21212, #64018 ) ;
#123043=CARTESIAN_POINT ( 'NONE',  ( -14.29289321881335262, 14.25929247661556509, 5.000000000000000000 ) ) ;
#123044=EDGE_LOOP ( 'NONE', ( #123917, #98220, #88333 ) ) ;
#123045=DIRECTION ( 'NONE',  ( 0.7071067811865486830, -0.7071067811865464625, -0.000000000000000000 ) ) ;
#123046=VERTEX_POINT ( 'NONE', #43771 ) ;
#123050=LINE ( 'NONE', #134655, #3556 ) ;
#123053=PLANE ( 'NONE',  #124690 ) ;
#123054=VERTEX_POINT ( 'NONE', #33634 ) ;
#123055=LINE ( 'NONE', #67243, #120963 ) ;
#123056=DIRECTION ( 'NONE',  ( 0.6830127018922181881, 0.6830127018922202975, -0.2588190451025214056 ) ) ;
#123058=DIRECTION ( 'NONE',  ( -0.7071067811865486830, -0.7071067811865464625, 0.000000000000000000 ) ) ;
#123060=VECTOR ( 'NONE', #126983, 1000.000000000000000 ) ;
#123063=VECTOR ( 'NONE', #71171, 1000.000000000000000 ) ;
#123065=ORIENTED_EDGE ( 'NONE', *, *, #35382, .T. ) ;
#123066=EDGE_CURVE ( 'NONE', #27137, #107840, #88723, .T. ) ;
#123067=ORIENTED_EDGE ( 'NONE', *, *, #128520, .T. ) ;
#123068=ADVANCED_FACE ( 'NONE', ( #23429 ), #22684, .T. ) ;
#123069=LINE ( 'NONE', #36750, #139269 ) ;
#123070=VERTEX_POINT ( 'NONE', #87985 ) ;
#123072=CARTESIAN_POINT ( 'NONE',  ( 51.29974487139158867, -27.71228299555242103, 4.000000000000000000 ) ) ;
#123073=DIRECTION ( 'NONE',  ( 0.000000000000000000, 0.000000000000000000, 1.000000000000000000 ) ) ;
#123074=CARTESIAN_POINT ( 'NONE',  ( -34.92500000000001137, -7.298069433178910437, 4.500000000000000888 ) ) ;
#123075=VECTOR ( 'NONE', #63138, 1000.000000000000000 ) ;
#123077=EDGE_LOOP ( 'NONE', ( #112712, #106143, #1582, #50778 ) ) ;
#123078=ADVANCED_FACE ( 'NONE', ( #122017 ), #132955, .F. ) ;
#123081=PLANE ( 'NONE',  #60429 ) ;
#123082=EDGE_CURVE ( 'NONE', #103031, #17161, #24158, .T. ) ;
#123083=PLANE ( 'NONE',  #110986 ) ;
#123084=ADVANCED_FACE ( 'NONE', ( #66954 ), #100300, .F. ) ;
#123085=PLANE ( 'NONE',  #133160 ) ;
#123086=ORIENTED_EDGE ( 'NONE', *, *, #44222, .F. ) ;
#123088=CARTESIAN_POINT ( 'NONE',  ( -63.18398860626900415, 28.73617430169831621, 5.000000000000000000 ) ) ;
#123089=AXIS2_PLACEMENT_3D ( 'NONE', #1770, #112722, #93116 ) ;
#123090=FACE_OUTER_BOUND ( 'NONE', #77025, .T. ) ;
#123092=DIRECTION ( 'NONE',  ( -0.7071067811865486830, 0.7071067811865464625, 0.000000000000000000 ) ) ;
#123094=VERTEX_POINT ( 'NONE', #110423 ) ;
#123097=ADVANCED_FACE ( 'NONE', ( #11097 ), #55373, .F. ) ;
#123098=VERTEX_POINT ( 'NONE', #108022 ) ;
#123099=ADVANCED_FACE ( 'NONE', ( #142831 ), #99294, .F. ) ;
#123100=CARTESIAN_POINT ( 'NONE',  ( 33.18398860626899705, 28.73617430169810305, 5.000000000000000000 ) ) ;
#123102=LINE ( 'NONE', #123824, #17948 ) ;
#123104=ORIENTED_EDGE ( 'NONE', *, *, #124533, .T. ) ;
#123105=VECTOR ( 'NONE', #78089, 1000.000000000000000 ) ;
#123106=EDGE_CURVE ( 'NONE', #101635, #64566, #96427, .T. ) ;
#123107=VECTOR ( 'NONE', #60992, 1000.000000000000000 ) ;
#123109=DIRECTION ( 'NONE',  ( 0.7071067811865487940, -0.7071067811865463515, 0.000000000000000000 ) ) ;
#123111=CARTESIAN_POINT ( 'NONE',  ( 25.49999999999982947, 3.052185695429136647, 5.000000000000000000 ) ) ;
#123114=ORIENTED_EDGE ( 'NONE', *, *, #50937, .T. ) ;
#123115=CARTESIAN_POINT ( 'NONE',  ( 15.56584921360887108, 8.021612662230191759, 4.000000000000000000 ) ) ;
#123117=VECTOR ( 'NONE', #3039, 1000.000000000000000 ) ;
#123123=EDGE_LOOP ( 'NONE', ( #22138, #59674, #93297, #22402 ) ) ;
#123125=PLANE ( 'NONE',  #53772 ) ;
#123127=DIRECTION ( 'NONE',  ( -0.000000000000000000, -0.3543493200069152693, 0.9351131265310292928 ) ) ;
#123128=VECTOR ( 'NONE', #27684, 1000.000000000000000 ) ;
#123130=CARTESIAN_POINT ( 'NONE',  ( 42.18398860626899705, 28.73617430169816700, 5.000000000000000000 ) ) ;
#123131=EDGE_CURVE ( 'NONE', #56643, #9187, #121065, .T. ) ;
#123132=CARTESIAN_POINT ( 'NONE',  ( -18.70710678118640047, -15.74070752338412760, 5.000000000000000000 ) ) ;
#123134=EDGE_CURVE ( 'NONE', #84461, #61441, #66015, .T. ) ;
#123135=ORIENTED_EDGE ( 'NONE', *, *, #98286, .T. ) ;
#123136=VERTEX_POINT ( 'NONE', #31228 ) ;
#123137=ORIENTED_EDGE ( 'NONE', *, *, #108259, .F. ) ;
#123139=EDGE_CURVE ( 'NONE', #73074, #63455, #130023, .T. ) ;
#123141=VECTOR ( 'NONE', #18406, 999.9999999999998863 ) ;
#123142=CARTESIAN_POINT ( 'NONE',  ( 34.92499999999998295, -22.22500000000000142, 4.500000000000000888 ) ) ;
#123143=ORIENTED_EDGE ( 'NONE', *, *, #87527, .F. ) ;
#123145=CARTESIAN_POINT ( 'NONE',  ( 60.18398860626900415, 28.73617430169829490, 5.000000000000000000 ) ) ;
#123146=AXIS2_PLACEMENT_3D ( 'NONE', #16708, #83409, #5799 ) ;
#123147=DIRECTION ( 'NONE',  ( -0.000000000000000000, 0.3543493200069153248, 0.9351131265310292928 ) ) ;
#123148=VECTOR ( 'NONE', #2315, 1000.000000000000000 ) ;
#123149=CARTESIAN_POINT ( 'NONE',  ( 27.48921356237309155, -27.52281430457074762, 5.000000000000000000 ) ) ;
#123150=VERTEX_POINT ( 'NONE', #63861 ) ;
#123151=CARTESIAN_POINT ( 'NONE',  ( -17.99999999999987566, 16.93112307739200872, 4.000000000000000000 ) ) ;
#123152=ORIENTED_EDGE ( 'NONE', *, *, #28086, .F. ) ;
#123153=DIRECTION ( 'NONE',  ( 1.000000000000000000, 0.000000000000000000, 0.000000000000000000 ) ) ;
#123154=ORIENTED_EDGE ( 'NONE', *, *, #27763, .T. ) ;
#123156=ORIENTED_EDGE ( 'NONE', *, *, #130123, .T. ) ;
#123157=LINE ( 'NONE', #67348, #108380 ) ;
#123158=ORIENTED_EDGE ( 'NONE', *, *, #48739, .F. ) ;
#123159=ORIENTED_EDGE ( 'NONE', *, *, #97745, .T. ) ;
#123160=VECTOR ( 'NONE', #21327, 999.9999999999998863 ) ;
#123162=CARTESIAN_POINT ( 'NONE',  ( -57.29974487139158157, -27.71228299555246011, 4.000000000000000000 ) ) ;
#123163=CARTESIAN_POINT ( 'NONE',  ( 31.82816939922330945, -2.240707523384262601, 4.000000000000000000 ) ) ;
#123166=EDGE_CURVE ( 'NONE', #56146, #14203, #87024, .T. ) ;
#123167=CARTESIAN_POINT ( 'NONE',  ( -54.18398860626899705, 28.73617430169825226, 5.000000000000000000 ) ) ;
#123168=VECTOR ( 'NONE', #138422, 1000.000000000000000 ) ;
#123169=CARTESIAN_POINT ( 'NONE',  ( -16.49999999999988276, -4.533600742197690714, 5.000000000000000000 ) ) ;
#123171=VECTOR ( 'NONE', #88288, 1000.000000000000000 ) ;
#123172=FACE_OUTER_BOUND ( 'NONE', #29438, .T. ) ;
#123173=VERTEX_POINT ( 'NONE', #109486 ) ;
#123175=DIRECTION ( 'NONE',  ( -0.6830127018922180770, -0.6830127018922204085, -0.2588190451025213501 ) ) ;
#123176=LINE ( 'NONE', #23851, #35683 ) ;
#123178=ORIENTED_EDGE ( 'NONE', *, *, #53910, .T. ) ;
#123179=AXIS2_PLACEMENT_3D ( 'NONE', #112491, #13146, #2257 ) ;
#123181=EDGE_LOOP ( 'NONE', ( #128100, #22703, #133568, #101362 ) ) ;
#123182=EDGE_CURVE ( 'NONE', #27059, #29014, #74010, .T. ) ;
#123183=ORIENTED_EDGE ( 'NONE', *, *, #102114, .T. ) ;
#123184=PLANE ( 'NONE',  #95385 ) ;
#123185=DIRECTION ( 'NONE',  ( -0.7071067811865487940, 0.7071067811865463515, 0.000000000000000000 ) ) ;
#123186=EDGE_CURVE ( 'NONE', #103613, #114421, #30511, .T. ) ;
#123187=LINE ( 'NONE', #37598, #101875 ) ;
#123188=DIRECTION ( 'NONE',  ( -0.7071067811865487940, 0.7071067811865463515, -0.000000000000000000 ) ) ;
#123190=FACE_OUTER_BOUND ( 'NONE', #70573, .T. ) ;
#123192=VERTEX_POINT ( 'NONE', #43516 ) ;
#123193=DIRECTION ( 'NONE',  ( 1.000000000000000000, 0.000000000000000000, 0.000000000000000000 ) ) ;
#123194=EDGE_CURVE ( 'NONE', #137919, #32809, #131971, .T. ) ;
#123195=ADVANCED_FACE ( 'NONE', ( #54425 ), #142140, .F. ) ;
#123197=ORIENTED_EDGE ( 'NONE', *, *, #130757, .T. ) ;
#123200=ADVANCED_FACE ( 'NONE', ( #84877 ), #98601, .F. ) ;
#123202=ORIENTED_EDGE ( 'NONE', *, *, #70082, .T. ) ;
#123203=VERTEX_POINT ( 'NONE', #18898 ) ;
#123205=DIRECTION ( 'NONE',  ( 0.7071067811865487940, -0.7071067811865463515, 0.000000000000000000 ) ) ;
#123206=PLANE ( 'NONE',  #32458 ) ;
#123207=FACE_OUTER_BOUND ( 'NONE', #94269, .T. ) ;
#123208=VECTOR ( 'NONE', #45151, 1000.000000000000227 ) ;
#123209=VECTOR ( 'NONE', #4172, 1000.000000000000000 ) ;
#123210=DIRECTION ( 'NONE',  ( 0.7071067811865487940, -0.7071067811865463515, 0.000000000000000000 ) ) ;
#123211=AXIS2_PLACEMENT_3D ( 'NONE', #130611, #142197, #755 ) ;
#123212=CARTESIAN_POINT ( 'NONE',  ( -54.18398860626899705, 28.73617430169825226, 5.000000000000000000 ) ) ;
#123213=ORIENTED_EDGE ( 'NONE', *, *, #69123, .T. ) ;
#123214=VECTOR ( 'NONE', #1515, 999.9999999999998863 ) ;
#123215=DIRECTION ( 'NONE',  ( -0.7071067811865486830, -0.7071067811865464625, 0.000000000000000000 ) ) ;
#123216=EDGE_CURVE ( 'NONE', #114730, #23765, #11436, .T. ) ;
#123217=VECTOR ( 'NONE', #15386, 1000.000000000000227 ) ;
#123220=VERTEX_POINT ( 'NONE', #97137 ) ;
#123221=VECTOR ( 'NONE', #132914, 1000.000000000000114 ) ;
#123222=VECTOR ( 'NONE', #111436, 999.9999999999998863 ) ;
#123223=EDGE_CURVE ( 'NONE', #139365, #89715, #141397, .T. ) ;
#123224=DIRECTION ( 'NONE',  ( -0.6830127018922180770, -0.6830127018922204085, -0.2588190451025213501 ) ) ;
#123225=ORIENTED_EDGE ( 'NONE', *, *, #134896, .T. ) ;
#123227=VERTEX_POINT ( 'NONE', #86324 ) ;
#123228=EDGE_LOOP ( 'NONE', ( #42739, #46426, #61893, #51430 ) ) ;
#123229=DIRECTION ( 'NONE',  ( -8.817971600062198362E-18, -0.3543493200069152693, 0.9351131265310292928 ) ) ;
#123230=DIRECTION ( 'NONE',  ( -0.6830127018922181881, 0.6830127018922202975, -0.2588190451025214056 ) ) ;
#123232=ORIENTED_EDGE ( 'NONE', *, *, #56140, .T. ) ;
#123234=EDGE_LOOP ( 'NONE', ( #134643, #111521, #65017, #104962 ) ) ;
#123236=DIRECTION ( 'NONE',  ( -0.7071067811865487940, 0.7071067811865463515, 0.000000000000000000 ) ) ;
#123237=DIRECTION ( 'NONE',  ( 0.7071067811865487940, 0.7071067811865463515, -0.000000000000000000 ) ) ;
#123238=PLANE ( 'NONE',  #60031 ) ;
#123240=PLANE ( 'NONE',  #90783 ) ;
#123241=LINE ( 'NONE', #23916, #77302 ) ;
#123242=EDGE_CURVE ( 'NONE', #37516, #42382, #71086, .T. ) ;
#123243=CARTESIAN_POINT ( 'NONE',  ( 9.489213562373095101, -27.52281430457062328, 5.000000000000000000 ) ) ;
#123247=DIRECTION ( 'NONE',  ( 0.7071067811865486830, -0.7071067811865464625, -0.000000000000000000 ) ) ;
#123248=CARTESIAN_POINT ( 'NONE',  ( 48.18398860626899705, 28.73617430169820608, 5.000000000000000000 ) ) ;
#123249=ORIENTED_EDGE ( 'NONE', *, *, #92070, .F. ) ;
#123251=VERTEX_POINT ( 'NONE', #126165 ) ;
#123252=EDGE_CURVE ( 'NONE', #11459, #91750, #82664, .T. ) ;
#123254=AXIS2_PLACEMENT_3D ( 'NONE', #21835, #31299, #84955 ) ;
#123255=ORIENTED_EDGE ( 'NONE', *, *, #61781, .F. ) ;
#123256=ORIENTED_EDGE ( 'NONE', *, *, #113890, .T. ) ;
#123257=ADVANCED_FACE ( 'NONE', ( #115230 ), #15916, .T. ) ;
#123258=EDGE_LOOP ( 'NONE', ( #124086, #96049, #2966, #143233 ) ) ;
#123259=CARTESIAN_POINT ( 'NONE',  ( -30.18398860626900060, 28.73617430169808173, 5.000000000000000000 ) ) ;
#123260=FACE_OUTER_BOUND ( 'NONE', #96001, .T. ) ;
#123262=PLANE ( 'NONE',  #19938 ) ;
#123263=ORIENTED_EDGE ( 'NONE', *, *, #64998, .T. ) ;
#123264=DIRECTION ( 'NONE',  ( 0.7071067811865487940, 0.7071067811865463515, 0.000000000000000000 ) ) ;
#123265=EDGE_CURVE ( 'NONE', #50158, #123707, #94230, .T. ) ;
#123266=CARTESIAN_POINT ( 'NONE',  ( -6.516654386410399624, 22.22500000000000142, 4.500000000000000888 ) ) ;
#123267=DIRECTION ( 'NONE',  ( -0.6830127018922180770, -0.6830127018922204085, -0.2588190451025213501 ) ) ;
#123269=ORIENTED_EDGE ( 'NONE', *, *, #50421, .T. ) ;
#123270=CARTESIAN_POINT ( 'NONE',  ( 20.20666063542138247, 21.75929247661549581, 4.998822639870702744 ) ) ;
#123271=CARTESIAN_POINT ( 'NONE',  ( -32.18650864602341954, -15.74070752338412760, 8.904080028139013336 ) ) ;
#123272=CARTESIAN_POINT ( 'NONE',  ( 5.510786437626906675, -27.52281430457051314, 5.000000000000000000 ) ) ;
#123273=CARTESIAN_POINT ( 'NONE',  ( 19.49999999999985789, -19.53360074219754594, 5.000000000000000000 ) ) ;
#123274=LINE ( 'NONE', #68203, #22111 ) ;
#123275=CARTESIAN_POINT ( 'NONE',  ( -16.49999999999988631, -7.420205493532911589, -2.617629953481292127 ) ) ;
#123276=CARTESIAN_POINT ( 'NONE',  ( 69.48921356237309510, -27.52281430457103895, 5.000000000000000000 ) ) ;
#123277=LINE ( 'NONE', #45722, #17460 ) ;
#123278=CARTESIAN_POINT ( 'NONE',  ( 42.18398860626899705, 28.73617430169816700, 5.000000000000000000 ) ) ;
#123279=ORIENTED_EDGE ( 'NONE', *, *, #135330, .F. ) ;
#123280=ORIENTED_EDGE ( 'NONE', *, *, #34181, .F. ) ;
#123283=ADVANCED_FACE ( 'NONE', ( #105797 ), #116706, .F. ) ;
#123284=VECTOR ( 'NONE', #56285, 1000.000000000000000 ) ;
#123285=CARTESIAN_POINT ( 'NONE',  ( -2.510786437626908008, -27.52281430457053446, 5.000000000000000000 ) ) ;
#123286=VECTOR ( 'NONE', #48508, 1000.000000000000000 ) ;
#123287=CARTESIAN_POINT ( 'NONE',  ( 36.18398860626899705, 28.73617430169812437, 5.000000000000000000 ) ) ;
#123289=CARTESIAN_POINT ( 'NONE',  ( 51.18398860626899705, 28.73617430169823095, 5.000000000000000000 ) ) ;
#123290=FACE_OUTER_BOUND ( 'NONE', #88365, .T. ) ;
#123294=VERTEX_POINT ( 'NONE', #129001 ) ;
#123297=LINE ( 'NONE', #57328, #50083 ) ;
#123298=( BOUNDED_CURVE ( )  B_SPLINE_CURVE ( 3, ( #44674, #19997, #45377, #109163 ),
 .UNSPECIFIED., .F., .T. ) 
 B_SPLINE_CURVE_WITH_KNOTS ( ( 4, 4 ),
 ( 1.208578181583235267, 1.359146454359472678 ),
 .UNSPECIFIED. ) 
 CURVE ( )  GEOMETRIC_REPRESENTATION_ITEM ( )  RATIONAL_B_SPLINE_CURVE ( ( 1.000000000000000000, 0.9981116584018945304, 0.9981116584018945304, 1.000000000000000000 ) ) 
 REPRESENTATION_ITEM ( '' )  );
#123299=ORIENTED_EDGE ( 'NONE', *, *, #117140, .F. ) ;
#123300=VERTEX_POINT ( 'NONE', #51465 ) ;
#123303=CARTESIAN_POINT ( 'NONE',  ( 45.18398860626900415, 28.73617430169818832, 5.000000000000000000 ) ) ;
#123304=AXIS2_PLACEMENT_3D ( 'NONE', #127715, #72660, #40702 ) ;
#123305=ADVANCED_FACE ( 'NONE', ( #5047 ), #7191, .F. ) ;
#123308=FACE_OUTER_BOUND ( 'NONE', #9567, .T. ) ;
#123309=EDGE_LOOP ( 'NONE', ( #98522, #31679, #133414, #17571 ) ) ;
#123310=ORIENTED_EDGE ( 'NONE', *, *, #67901, .F. ) ;
#123311=AXIS2_PLACEMENT_3D ( 'NONE', #63683, #54935, #129611 ) ;
#123312=VECTOR ( 'NONE', #42263, 1000.000000000000000 ) ;
#123313=ORIENTED_EDGE ( 'NONE', *, *, #117460, .T. ) ;
#123314=AXIS2_PLACEMENT_3D ( 'NONE', #90115, #90865, #12552 ) ;
#123315=VECTOR ( 'NONE', #126535, 1000.000000000000000 ) ;
#123316=VECTOR ( 'NONE', #7193, 999.9999999999998863 ) ;
#123319=ORIENTED_EDGE ( 'NONE', *, *, #133595, .F. ) ;
#123320=CARTESIAN_POINT ( 'NONE',  ( -4.171830600776450737, -17.24070752338411694, 4.000000000000000000 ) ) ;
#123321=VECTOR ( 'NONE', #97179, 1000.000000000000000 ) ;
#123322=FACE_OUTER_BOUND ( 'NONE', #99099, .T. ) ;
#123323=VECTOR ( 'NONE', #3046, 1000.000000000000227 ) ;
#123326=CARTESIAN_POINT ( 'NONE',  ( -30.79289321881324071, 3.759292476615681888, 5.000000000000000000 ) ) ;
#123327=FACE_BOUND ( 'NONE', #60337, .T. ) ;
#123329=DIRECTION ( 'NONE',  ( 0.7071067811865486830, -0.7071067811865464625, -0.000000000000000000 ) ) ;
#123330=DIRECTION ( 'NONE',  ( 0.3543493200069163240, 0.000000000000000000, 0.9351131265310288487 ) ) ;
#123331=LINE ( 'NONE', #55930, #118522 ) ;
#123332=CARTESIAN_POINT ( 'NONE',  ( -19.83957586139685247, 9.091547215995101183, 4.000000000000000000 ) ) ;
#123333=ORIENTED_EDGE ( 'NONE', *, *, #57901, .T. ) ;
#123334=FACE_OUTER_BOUND ( 'NONE', #72274, .T. ) ;
#123336=ORIENTED_EDGE ( 'NONE', *, *, #104208, .T. ) ;
#123337=VERTEX_POINT ( 'NONE', #38442 ) ;
#123339=ORIENTED_EDGE ( 'NONE', *, *, #107466, .T. ) ;
#123340=AXIS2_PLACEMENT_3D ( 'NONE', #101802, #143167, #90208 ) ;
#123341=LINE ( 'NONE', #45088, #92680 ) ;
#123342=CARTESIAN_POINT ( 'NONE',  ( -25.82816939922335209, -14.24070752338413293, 4.000000000000000000 ) ) ;
#123343=ORIENTED_EDGE ( 'NONE', *, *, #85761, .F. ) ;
#123344=CARTESIAN_POINT ( 'NONE',  ( 34.92499999999998295, 18.94777415420114508, 3.758136617891463249 ) ) ;
#123345=DIRECTION ( 'NONE',  ( -0.6830127018922181881, 0.6830127018922202975, -0.2588190451025214056 ) ) ;
#123346=AXIS2_PLACEMENT_3D ( 'NONE', #42763, #76825, #110110 ) ;
#123348=LINE ( 'NONE', #805, #74095 ) ;
#123349=LINE ( 'NONE', #68277, #8913 ) ;
#123350=VECTOR ( 'NONE', #32427, 1000.000000000000000 ) ;
#123352=ORIENTED_EDGE ( 'NONE', *, *, #30927, .F. ) ;
#123353=EDGE_CURVE ( 'NONE', #72974, #139938, #84116, .T. ) ;
#123354=ORIENTED_EDGE ( 'NONE', *, *, #122185, .F. ) ;
#123356=VECTOR ( 'NONE', #122330, 1000.000000000000000 ) ;
#123357=VERTEX_POINT ( 'NONE', #117388 ) ;
#123359=LINE ( 'NONE', #34915, #130676 ) ;
#123360=VERTEX_POINT ( 'NONE', #83377 ) ;
#123363=CARTESIAN_POINT ( 'NONE',  ( 36.18398860626899705, 28.73617430169812437, 5.000000000000000000 ) ) ;
#123364=EDGE_CURVE ( 'NONE', #118176, #18168, #49348, .T. ) ;
#123365=EDGE_CURVE ( 'NONE', #91404, #1467, #27535, .T. ) ;
#123366=CARTESIAN_POINT ( 'NONE',  ( 30.29974487139158867, -27.71228299555227537, 4.000000000000000000 ) ) ;
#123368=CARTESIAN_POINT ( 'NONE',  ( -8.999999999999939604, 16.93112307739201938, 4.000000000000000000 ) ) ;
#123369=PLANE ( 'NONE',  #111595 ) ;
#123370=EDGE_CURVE ( 'NONE', #130889, #54158, #16671, .T. ) ;
#123371=EDGE_CURVE ( 'NONE', #79780, #57963, #127589, .T. ) ;
#123373=FACE_OUTER_BOUND ( 'NONE', #36275, .T. ) ;
#123376=PLANE ( 'NONE',  #82374 ) ;
#123377=EDGE_CURVE ( 'NONE', #49398, #135194, #84793, .T. ) ;
#123378=FACE_OUTER_BOUND ( 'NONE', #104967, .T. ) ;
#123382=DIRECTION ( 'NONE',  ( -0.7071067811865486830, -0.7071067811865464625, 0.000000000000000000 ) ) ;
#123383=DIRECTION ( 'NONE',  ( -0.3543493200069162685, -0.000000000000000000, -0.9351131265310288487 ) ) ;
#123384=ORIENTED_EDGE ( 'NONE', *, *, #26724, .T. ) ;
#123385=CARTESIAN_POINT ( 'NONE',  ( 0.000000000000000000, 0.000000000000000000, 5.000000000000000000 ) ) ;
#123387=ORIENTED_EDGE ( 'NONE', *, *, #50584, .T. ) ;
#123388=ADVANCED_FACE ( 'NONE', ( #73918 ), #106509, .T. ) ;
#123391=DIRECTION ( 'NONE',  ( -0.6830127018922180770, -0.6830127018922204085, -0.2588190451025213501 ) ) ;
#123392=CARTESIAN_POINT ( 'NONE',  ( 18.00548008471250583, 28.92564299267925776, 4.000000000000000000 ) ) ;
#123393=VERTEX_POINT ( 'NONE', #137034 ) ;
#123394=DIRECTION ( 'NONE',  ( -0.000000000000000000, 0.000000000000000000, 1.000000000000000000 ) ) ;
#123396=CARTESIAN_POINT ( 'NONE',  ( 9.183988606268997046, 28.73617430169793607, 5.000000000000000000 ) ) ;
#123397=CARTESIAN_POINT ( 'NONE',  ( -21.32816939922337696, -12.74070752338415602, 4.000000000000000000 ) ) ;
#123399=AXIS2_PLACEMENT_3D ( 'NONE', #31642, #122189, #33798 ) ;
#123400=DIRECTION ( 'NONE',  ( -0.3543493200069162685, -0.000000000000000000, -0.9351131265310288487 ) ) ;
#123401=VERTEX_POINT ( 'NONE', #37740 ) ;
#123402=EDGE_CURVE ( 'NONE', #94958, #125587, #131152, .T. ) ;
#123403=DIRECTION ( 'NONE',  ( 0.6830127018922180770, -0.6830127018922204085, -0.2588190451025213501 ) ) ;
#123405=ORIENTED_EDGE ( 'NONE', *, *, #32992, .F. ) ;
#123406=ORIENTED_EDGE ( 'NONE', *, *, #105314, .F. ) ;
#123408=CARTESIAN_POINT ( 'NONE',  ( 2.510786437626908008, -27.52281430457053446, 5.000000000000000000 ) ) ;
#123411=ORIENTED_EDGE ( 'NONE', *, *, #119086, .T. ) ;
#123412=LINE ( 'NONE', #127475, #4162 ) ;
#123414=LINE ( 'NONE', #121927, #93171 ) ;
#123415=ORIENTED_EDGE ( 'NONE', *, *, #92583, .F. ) ;
#123416=CARTESIAN_POINT ( 'NONE',  ( -11.99999999999992006, -13.39766691384885000, -10.96608748226462993 ) ) ;
#123418=CARTESIAN_POINT ( 'NONE',  ( 23.99999999999983302, 9.631307414974347836, -9.079085613539486843 ) ) ;
#123419=ADVANCED_FACE ( 'NONE', ( #42743 ), #97804, .F. ) ;
#123420=VECTOR ( 'NONE', #16924, 1000.000000000000227 ) ;
#123421=CARTESIAN_POINT ( 'NONE',  ( -51.29974487139158867, -27.71228299555242103, 4.000000000000000000 ) ) ;
#123423=LINE ( 'NONE', #134275, #129864 ) ;
#123425=ORIENTED_EDGE ( 'NONE', *, *, #7395, .T. ) ;
#123426=VECTOR ( 'NONE', #35091, 1000.000000000000000 ) ;
#123427=VERTEX_POINT ( 'NONE', #53606 ) ;
#123428=ORIENTED_EDGE ( 'NONE', *, *, #104362, .T. ) ;
#123429=EDGE_CURVE ( 'NONE', #29014, #9981, #19531, .T. ) ;
#123431=ORIENTED_EDGE ( 'NONE', *, *, #78841, .F. ) ;
#123432=ADVANCED_FACE ( 'NONE', ( #76063 ), #142743, .F. ) ;
#123433=VERTEX_POINT ( 'NONE', #109395 ) ;
#123434=VECTOR ( 'NONE', #100345, 1000.000000000000000 ) ;
#123435=AXIS2_PLACEMENT_3D ( 'NONE', #67264, #46247, #2689 ) ;
#123438=DIRECTION ( 'NONE',  ( -0.000000000000000000, -0.3543493200069153248, -0.9351131265310291818 ) ) ;
#123441=LINE ( 'NONE', #103762, #120298 ) ;
#123442=LINE ( 'NONE', #133578, #95248 ) ;
#123445=DIRECTION ( 'NONE',  ( 0.7071067811865487940, 0.7071067811865463515, 0.000000000000000000 ) ) ;
#123447=EDGE_LOOP ( 'NONE', ( #25404, #39532, #52684, #29198 ) ) ;
#123448=DIRECTION ( 'NONE',  ( -0.000000000000000000, -0.000000000000000000, 1.000000000000000000 ) ) ;
#123449=LINE ( 'NONE', #87216, #28312 ) ;
#123454=DIRECTION ( 'NONE',  ( 0.7071067811865486830, -0.7071067811865464625, -0.000000000000000000 ) ) ;
#123456=DIRECTION ( 'NONE',  ( -0.7071067811865486830, -0.7071067811865464625, -0.000000000000000000 ) ) ;
#123457=VECTOR ( 'NONE', #37828, 1000.000000000000227 ) ;
#123458=CARTESIAN_POINT ( 'NONE',  ( 48.48921356237309510, -27.52281430457089328, 5.000000000000000000 ) ) ;
#123459=ORIENTED_EDGE ( 'NONE', *, *, #18785, .T. ) ;
#123460=VERTEX_POINT ( 'NONE', #21680 ) ;
#123462=EDGE_CURVE ( 'NONE', #81589, #133341, #98519, .T. ) ;
#123463=DIRECTION ( 'NONE',  ( -0.7071067811865486830, -0.7071067811865464625, 0.000000000000000000 ) ) ;
#123464=ORIENTED_EDGE ( 'NONE', *, *, #73842, .F. ) ;
#123466=AXIS2_PLACEMENT_3D ( 'NONE', #54361, #65230, #111555 ) ;
#123467=CARTESIAN_POINT ( 'NONE',  ( 0.000000000000000000, 0.000000000000000000, 5.000000000000000000 ) ) ;
#123469=EDGE_CURVE ( 'NONE', #110421, #137557, #131874, .T. ) ;
#123470=VECTOR ( 'NONE', #72784, 1000.000000000000000 ) ;
#123471=EDGE_LOOP ( 'NONE', ( #103704, #68982, #120095, #69336 ) ) ;
#123472=LINE ( 'NONE', #79976, #17754 ) ;
#123473=ORIENTED_EDGE ( 'NONE', *, *, #9604, .F. ) ;
#123475=DIRECTION ( 'NONE',  ( -0.7071067811865487940, 0.7071067811865463515, -0.000000000000000000 ) ) ;
#123478=PLANE ( 'NONE',  #99614 ) ;
#123479=VERTEX_POINT ( 'NONE', #30418 ) ;
#123481=CARTESIAN_POINT ( 'NONE',  ( -4.637538124160927921, 22.22499999999999432, 4.000000000000000000 ) ) ;
#123482=VERTEX_POINT ( 'NONE', #32568 ) ;
#123484=LINE ( 'NONE', #2346, #29988 ) ;
#123486=DIRECTION ( 'NONE',  ( -0.7071067811865487940, 0.7071067811865463515, -0.000000000000000000 ) ) ;
#123487=( BOUNDED_CURVE ( )  B_SPLINE_CURVE ( 3, ( #1975, #2732, #13589, #49127 ),
 .UNSPECIFIED., .F., .T. ) 
 B_SPLINE_CURVE_WITH_KNOTS ( ( 4, 4 ),
 ( 2.001653308786160768, 3.503810798801450854 ),
 .UNSPECIFIED. ) 
 CURVE ( )  GEOMETRIC_REPRESENTATION_ITEM ( )  RATIONAL_B_SPLINE_CURVE ( ( 1.000000000000000000, 0.8206354192515221690, 0.8206354192515221690, 1.000000000000000000 ) ) 
 REPRESENTATION_ITEM ( '' )  );
#123488=AXIS2_PLACEMENT_3D ( 'NONE', #54411, #30498, #120305 ) ;
#123489=ORIENTED_EDGE ( 'NONE', *, *, #13694, .F. ) ;
#123490=VECTOR ( 'NONE', #130158, 1000.000000000000000 ) ;
#123491=CARTESIAN_POINT ( 'NONE',  ( 27.29974487139158512, -27.71228299555225405, 4.000000000000000000 ) ) ;
#123493=DIRECTION ( 'NONE',  ( -0.6830127018922180770, -0.6830127018922204085, -0.2588190451025213501 ) ) ;
#123494=CARTESIAN_POINT ( 'NONE',  ( -20.99999999999985789, 9.631307414974306980, -9.079085613539588095 ) ) ;
#123495=ORIENTED_EDGE ( 'NONE', *, *, #7869, .F. ) ;
#123496=VERTEX_POINT ( 'NONE', #140585 ) ;
#123497=AXIS2_PLACEMENT_3D ( 'NONE', #90989, #48178, #46806 ) ;
#123498=LINE ( 'NONE', #24152, #116420 ) ;
#123499=ORIENTED_EDGE ( 'NONE', *, *, #31678, .T. ) ;
#123500=EDGE_CURVE ( 'NONE', #38910, #18784, #110094, .T. ) ;
#123501=EDGE_CURVE ( 'NONE', #137039, #60934, #31145, .T. ) ;
#123502=FACE_OUTER_BOUND ( 'NONE', #47558, .T. ) ;
#123503=ORIENTED_EDGE ( 'NONE', *, *, #107182, .T. ) ;
#123504=LINE ( 'NONE', #25570, #141837 ) ;
#123505=CARTESIAN_POINT ( 'NONE',  ( 34.92499999999998295, 22.22500000000000142, 5.000000000000000000 ) ) ;
#123506=CARTESIAN_POINT ( 'NONE',  ( -22.42819999999999681, 3.174999999999997602, 5.000000000000000000 ) ) ;
#123507=VECTOR ( 'NONE', #78712, 1000.000000000000000 ) ;
#123508=PLANE ( 'NONE',  #104370 ) ;
#123509=FACE_BOUND ( 'NONE', #709, .T. ) ;
#123510=EDGE_CURVE ( 'NONE', #60942, #64740, #108644, .T. ) ;
#123511=DIRECTION ( 'NONE',  ( 0.7071067811865487940, 0.7071067811865463515, 0.000000000000000000 ) ) ;
#123512=LINE ( 'NONE', #45937, #134716 ) ;
#123513=AXIS2_PLACEMENT_3D ( 'NONE', #131652, #129482, #65719 ) ;
#123514=DIRECTION ( 'NONE',  ( -0.000000000000000000, -0.3543493200069152693, 0.9351131265310292928 ) ) ;
#123515=LINE ( 'NONE', #89419, #69010 ) ;
#123516=VERTEX_POINT ( 'NONE', #99204 ) ;
#123517=CARTESIAN_POINT ( 'NONE',  ( 0.000000000000000000, 0.000000000000000000, 5.000000000000000000 ) ) ;
#123518=ORIENTED_EDGE ( 'NONE', *, *, #29273, .F. ) ;
#123521=VERTEX_POINT ( 'NONE', #47753 ) ;
#123522=CARTESIAN_POINT ( 'NONE',  ( -20.25795612380215971, -2.670494247963030698, 4.000000000000000000 ) ) ;
#123523=ORIENTED_EDGE ( 'NONE', *, *, #86084, .F. ) ;
#123524=CARTESIAN_POINT ( 'NONE',  ( -18.18398860626898994, 28.73617430169800002, 5.000000000000000000 ) ) ;
#123525=AXIS2_PLACEMENT_3D ( 'NONE', #83445, #116766, #73989 ) ;
#123526=VECTOR ( 'NONE', #105822, 1000.000000000000000 ) ;
#123527=DIRECTION ( 'NONE',  ( 0.7071067811865486830, -0.7071067811865464625, -0.000000000000000000 ) ) ;
#123528=LINE ( 'NONE', #124208, #84801 ) ;
#123531=LINE ( 'NONE', #34351, #19456 ) ;
#123532=DIRECTION ( 'NONE',  ( 0.6830127018922180770, -0.6830127018922204085, -0.2588190451025213501 ) ) ;
#123533=CARTESIAN_POINT ( 'NONE',  ( 5.999999999999963585, 17.96639925780208458, 5.000000000000000000 ) ) ;
#123534=VERTEX_POINT ( 'NONE', #124560 ) ;
#123535=AXIS2_PLACEMENT_3D ( 'NONE', #82125, #5208, #4448 ) ;
#123536=EDGE_LOOP ( 'NONE', ( #87709, #138355, #104796, #125961 ) ) ;
#123537=DIRECTION ( 'NONE',  ( 1.000000000000000000, 0.000000000000000000, 0.000000000000000000 ) ) ;
#123539=VERTEX_POINT ( 'NONE', #111535 ) ;
#123540=ORIENTED_EDGE ( 'NONE', *, *, #1137, .F. ) ;
#123543=FACE_OUTER_BOUND ( 'NONE', #35378, .T. ) ;
#123544=ORIENTED_EDGE ( 'NONE', *, *, #52456, .F. ) ;
#123545=PLANE ( 'NONE',  #9182 ) ;
#123548=EDGE_CURVE ( 'NONE', #133840, #100802, #91921, .T. ) ;
#123550=VECTOR ( 'NONE', #117307, 1000.000000000000000 ) ;
#123552=CARTESIAN_POINT ( 'NONE',  ( -28.82816939922332011, -8.240707523384200428, 4.000000000000000000 ) ) ;
#123553=ADVANCED_FACE ( 'NONE', ( #66622 ), #36141, .T. ) ;
#123554=VERTEX_POINT ( 'NONE', #77515 ) ;
#123555=LINE ( 'NONE', #114065, #6362 ) ;
#123556=EDGE_CURVE ( 'NONE', #134614, #86498, #113674, .T. ) ;
#123557=DIRECTION ( 'NONE',  ( -0.7071067811865486830, 0.7071067811865464625, 0.000000000000000000 ) ) ;
#123558=DIRECTION ( 'NONE',  ( -0.7071067811865487940, 0.7071067811865463515, -0.000000000000000000 ) ) ;
#123560=EDGE_LOOP ( 'NONE', ( #99559, #134498, #40380, #90515 ) ) ;
#123561=ORIENTED_EDGE ( 'NONE', *, *, #73514, .F. ) ;
#123562=EDGE_CURVE ( 'NONE', #87598, #122913, #56500, .T. ) ;
#123564=CARTESIAN_POINT ( 'NONE',  ( 45.29974487139158867, -27.71228299555237840, 4.000000000000000000 ) ) ;
#123565=VECTOR ( 'NONE', #57752, 1000.000000000000000 ) ;
#123566=CARTESIAN_POINT ( 'NONE',  ( 19.49999999999986500, -13.91253812416061386, 4.000000000000000000 ) ) ;
#123567=VERTEX_POINT ( 'NONE', #22355 ) ;
#123570=EDGE_CURVE ( 'NONE', #84117, #66120, #44912, .T. ) ;
#123571=AXIS2_PLACEMENT_3D ( 'NONE', #134421, #2430, #113344 ) ;
#123572=EDGE_CURVE ( 'NONE', #4279, #42711, #134757, .T. ) ;
#123574=DIRECTION ( 'NONE',  ( -0.000000000000000000, -0.3543493200069152693, 0.9351131265310292928 ) ) ;
#123575=DIRECTION ( 'NONE',  ( -0.6830127018922181881, 0.6830127018922202975, -0.2588190451025214056 ) ) ;
#123577=CARTESIAN_POINT ( 'NONE',  ( 39.48921356237310221, -27.52281430457082934, 5.000000000000000000 ) ) ;
#123579=VECTOR ( 'NONE', #9584, 1000.000000000000227 ) ;
#123580=ADVANCED_FACE ( 'NONE', ( #80370 ), #14370, .F. ) ;
#123581=DIRECTION ( 'NONE',  ( -0.7071067811865486830, -0.7071067811865464625, -0.000000000000000000 ) ) ;
#123582=DIRECTION ( 'NONE',  ( 0.7071067811865486830, -0.7071067811865464625, -0.000000000000000000 ) ) ;
#123584=ORIENTED_EDGE ( 'NONE', *, *, #10585, .T. ) ;
#123585=ORIENTED_EDGE ( 'NONE', *, *, #111619, .T. ) ;
#123588=ADVANCED_FACE ( 'NONE', ( #11476 ), #67344, .F. ) ;
#123589=VECTOR ( 'NONE', #129522, 1000.000000000000000 ) ;
#123590=DIRECTION ( 'NONE',  ( -1.000000000000000000, 0.000000000000000000, -0.000000000000000000 ) ) ;
#123591=ORIENTED_EDGE ( 'NONE', *, *, #66907, .T. ) ;
#123593=CARTESIAN_POINT ( 'NONE',  ( 63.29974487139158867, -27.71228299555250274, 4.000000000000000000 ) ) ;
#123594=CARTESIAN_POINT ( 'NONE',  ( -6.489213562373093325, -27.52281430457059841, 5.000000000000000000 ) ) ;
#123595=ORIENTED_EDGE ( 'NONE', *, *, #140447, .F. ) ;
#123596=CARTESIAN_POINT ( 'NONE',  ( -8.999999999999937828, -7.068876922607741697, 4.000000000000000000 ) ) ;
#123597=DIRECTION ( 'NONE',  ( -0.000000000000000000, -0.3543493200069152693, 0.9351131265310292928 ) ) ;
#123600=FACE_OUTER_BOUND ( 'NONE', #121461, .T. ) ;
#123606=ORIENTED_EDGE ( 'NONE', *, *, #139122, .T. ) ;
#123610=PLANE ( 'NONE',  #32673 ) ;
#123613=CARTESIAN_POINT ( 'NONE',  ( 26.29298673570676215, -21.74070752338406365, 4.999753212805220670 ) ) ;
#123614=ORIENTED_EDGE ( 'NONE', *, *, #103162, .T. ) ;
#123616=ORIENTED_EDGE ( 'NONE', *, *, #53156, .F. ) ;
#123617=DIRECTION ( 'NONE',  ( 0.7071067811865487940, 0.7071067811865463515, 0.000000000000000000 ) ) ;
#123618=FACE_OUTER_BOUND ( 'NONE', #78284, .T. ) ;
#123619=LINE ( 'NONE', #56932, #135339 ) ;
#123620=ADVANCED_FACE ( 'NONE', ( #2769 ), #617, .F. ) ;
#123621=CARTESIAN_POINT ( 'NONE',  ( -36.29974487139159578, -27.71228299555231445, 4.000000000000000000 ) ) ;
#123623=CARTESIAN_POINT ( 'NONE',  ( 24.18398860626899705, 28.73617430169804265, 5.000000000000000000 ) ) ;
#123624=AXIS2_PLACEMENT_3D ( 'NONE', #127820, #138696, #61173 ) ;
#123625=CARTESIAN_POINT ( 'NONE',  ( -57.48921356237308800, -27.52281430457095368, 5.000000000000000000 ) ) ;
#123626=ORIENTED_EDGE ( 'NONE', *, *, #136295, .F. ) ;
#123628=DIRECTION ( 'NONE',  ( -0.6830127018922180770, -0.6830127018922204085, -0.2588190451025213501 ) ) ;
#123630=CARTESIAN_POINT ( 'NONE',  ( -34.92500000000001137, 9.006123077391837484, 4.000000000000000000 ) ) ;
#123631=DIRECTION ( 'NONE',  ( -0.6830127018922181881, 0.6830127018922202975, -0.2588190451025214056 ) ) ;
#123632=ORIENTED_EDGE ( 'NONE', *, *, #64921, .F. ) ;
#123633=VECTOR ( 'NONE', #70908, 1000.000000000000000 ) ;
#123634=DIRECTION ( 'NONE',  ( 1.000000000000000000, 0.000000000000000000, 0.000000000000000000 ) ) ;
#123635=EDGE_CURVE ( 'NONE', #86443, #124077, #112865, .T. ) ;
#123639=ORIENTED_EDGE ( 'NONE', *, *, #41833, .T. ) ;
#123640=LINE ( 'NONE', #24987, #130923 ) ;
#123641=CARTESIAN_POINT ( 'NONE',  ( -42.48921356237308800, -27.52281430457085065, 5.000000000000000000 ) ) ;
#123644=LINE ( 'NONE', #59116, #138882 ) ;
#123645=DIRECTION ( 'NONE',  ( 0.7071067811865487940, 0.7071067811865463515, -0.000000000000000000 ) ) ;
#123646=VERTEX_POINT ( 'NONE', #127402 ) ;
#123647=LINE ( 'NONE', #59119, #99311 ) ;
#123648=FACE_OUTER_BOUND ( 'NONE', #67221, .T. ) ;
#123649=CARTESIAN_POINT ( 'NONE',  ( -24.21271579574130683, 0.1791150535437372460, 5.000000000000000000 ) ) ;
#123650=VECTOR ( 'NONE', #113491, 1000.000000000000000 ) ;
#123651=ORIENTED_EDGE ( 'NONE', *, *, #126008, .F. ) ;
#123652=ORIENTED_EDGE ( 'NONE', *, *, #112562, .T. ) ;
#123654=AXIS2_PLACEMENT_3D ( 'NONE', #79243, #90805, #113962 ) ;
#123655=ORIENTED_EDGE ( 'NONE', *, *, #66422, .F. ) ;
#123657=CARTESIAN_POINT ( 'NONE',  ( 24.48921356237309510, -27.52281430457072631, 5.000000000000000000 ) ) ;
#123658=DIRECTION ( 'NONE',  ( -0.7071067811865486830, -0.7071067811865464625, 0.000000000000000000 ) ) ;
#123660=CARTESIAN_POINT ( 'NONE',  ( -34.42500000000001137, 4.541399257801965739, 5.000000000000000000 ) ) ;
#123661=ORIENTED_EDGE ( 'NONE', *, *, #142991, .T. ) ;
#123662=ORIENTED_EDGE ( 'NONE', *, *, #57914, .F. ) ;
#123663=CARTESIAN_POINT ( 'NONE',  ( -20.25795612380215971, -2.670494247963030698, 4.000000000000000000 ) ) ;
#123665=EDGE_CURVE ( 'NONE', #118195, #131632, #26672, .T. ) ;
#123666=ORIENTED_EDGE ( 'NONE', *, *, #124207, .F. ) ;
#123667=EDGE_CURVE ( 'NONE', #61349, #60272, #95486, .T. ) ;
#123668=VECTOR ( 'NONE', #63129, 1000.000000000000227 ) ;
#123670=CARTESIAN_POINT ( 'NONE',  ( -10.49999999999992362, -4.533600742197692490, 5.000000000000000000 ) ) ;
#123671=CARTESIAN_POINT ( 'NONE',  ( -66.29974487139159578, -27.71228299555252406, 4.000000000000000000 ) ) ;
#123672=ORIENTED_EDGE ( 'NONE', *, *, #6442, .F. ) ;
#123674=FACE_BOUND ( 'NONE', #54994, .T. ) ;
#123675=ADVANCED_FACE ( 'NONE', ( #7010 ), #28104, .F. ) ;
#123676=LINE ( 'NONE', #68576, #77994 ) ;
#123677=DIRECTION ( 'NONE',  ( -0.7071067811865487940, 0.7071067811865463515, 0.000000000000000000 ) ) ;
#123678=DIRECTION ( 'NONE',  ( 1.000000000000000000, 0.000000000000000000, 0.000000000000000000 ) ) ;
#123679=LINE ( 'NONE', #80876, #57332 ) ;
#123680=VECTOR ( 'NONE', #22709, 1000.000000000000000 ) ;
#123681=CARTESIAN_POINT ( 'NONE',  ( -28.49999999999980460, 21.05218569542895324, 5.000000000000000000 ) ) ;
#123684=ORIENTED_EDGE ( 'NONE', *, *, #73732, .F. ) ;
#123686=ORIENTED_EDGE ( 'NONE', *, *, #67957, .T. ) ;
#123687=CARTESIAN_POINT ( 'NONE',  ( -2.510786437626908008, -27.52281430457053446, 5.000000000000000000 ) ) ;
#123688=EDGE_LOOP ( 'NONE', ( #95784, #29572, #114559, #9781 ) ) ;
#123690=CARTESIAN_POINT ( 'NONE',  ( 10.49999999999993250, 10.94296225409028089, -9.576120664313233277 ) ) ;
#123692=FACE_OUTER_BOUND ( 'NONE', #9664, .T. ) ;
#123693=ORIENTED_EDGE ( 'NONE', *, *, #137874, .T. ) ;
#123695=DIRECTION ( 'NONE',  ( 0.6830127018922181881, 0.6830127018922202975, -0.2588190451025214056 ) ) ;
#123697=DIRECTION ( 'NONE',  ( -0.000000000000000000, -0.3543493200069152693, 0.9351131265310292928 ) ) ;
#123698=DIRECTION ( 'NONE',  ( 0.7071067811865487940, -0.7071067811865463515, 0.000000000000000000 ) ) ;
#123699=CARTESIAN_POINT ( 'NONE',  ( 36.48921356237310221, -27.52281430457080802, 5.000000000000000000 ) ) ;
#123700=VECTOR ( 'NONE', #62224, 999.9999999999998863 ) ;
#123701=LINE ( 'NONE', #124385, #51424 ) ;
#123702=ORIENTED_EDGE ( 'NONE', *, *, #48085, .F. ) ;
#123703=DIRECTION ( 'NONE',  ( -0.6830127018922181881, 0.6830127018922202975, -0.2588190451025214056 ) ) ;
#123704=LINE ( 'NONE', #54870, #95130 ) ;
#123705=ORIENTED_EDGE ( 'NONE', *, *, #79035, .F. ) ;
#123706=ORIENTED_EDGE ( 'NONE', *, *, #126456, .T. ) ;
#123707=VERTEX_POINT ( 'NONE', #72369 ) ;
#123709=VERTEX_POINT ( 'NONE', #5605 ) ;
#123711=EDGE_CURVE ( 'NONE', #13955, #49848, #49163, .T. ) ;
#123714=CARTESIAN_POINT ( 'NONE',  ( 38.99451991528749062, 28.92564299267965211, 4.000000000000000000 ) ) ;
#123715=ORIENTED_EDGE ( 'NONE', *, *, #61866, .F. ) ;
#123716=ADVANCED_FACE ( 'NONE', ( #92621 ), #48424, .F. ) ;
#123717=CARTESIAN_POINT ( 'NONE',  ( -42.48921356237308800, -27.52281430457085065, 5.000000000000000000 ) ) ;
#123718=EDGE_CURVE ( 'NONE', #47033, #29497, #104939, .T. ) ;
#123719=VERTEX_POINT ( 'NONE', #38270 ) ;
#123720=DIRECTION ( 'NONE',  ( 0.7071067811865487940, 0.7071067811865463515, 0.000000000000000000 ) ) ;
#123721=ORIENTED_EDGE ( 'NONE', *, *, #68903, .F. ) ;
#123722=EDGE_CURVE ( 'NONE', #57991, #55512, #6289, .T. ) ;
#123724=LINE ( 'NONE', #24381, #85459 ) ;
#123725=LINE ( 'NONE', #102678, #33647 ) ;
#123726=EDGE_LOOP ( 'NONE', ( #52029, #27274, #106677 ) ) ;
#123727=CARTESIAN_POINT ( 'NONE',  ( 27.29974487139158512, -27.71228299555225405, 4.000000000000000000 ) ) ;
#123728=ORIENTED_EDGE ( 'NONE', *, *, #82804, .F. ) ;
#123730=ORIENTED_EDGE ( 'NONE', *, *, #120519, .F. ) ;
#123732=EDGE_CURVE ( 'NONE', #34094, #26993, #4132, .T. ) ;
#123733=LINE ( 'NONE', #136007, #72576 ) ;
#123734=CARTESIAN_POINT ( 'NONE',  ( 30.18398860626900060, 28.73617430169808173, 5.000000000000000000 ) ) ;
#123735=ADVANCED_FACE ( 'NONE', ( #39719 ), #106338, .F. ) ;
#123736=CARTESIAN_POINT ( 'NONE',  ( -27.48921356237309155, -27.52281430457074762, 5.000000000000000000 ) ) ;
#123739=FACE_OUTER_BOUND ( 'NONE', #68602, .T. ) ;
#123740=EDGE_CURVE ( 'NONE', #142010, #136110, #95720, .T. ) ;
#123741=VECTOR ( 'NONE', #61068, 1000.000000000000114 ) ;
#123743=DIRECTION ( 'NONE',  ( 0.7071067811865486830, -0.7071067811865464625, -0.000000000000000000 ) ) ;
#123744=FACE_OUTER_BOUND ( 'NONE', #63607, .T. ) ;
#123745=DIRECTION ( 'NONE',  ( -0.7071067811865486830, -0.7071067811865464625, 0.000000000000000000 ) ) ;
#123746=ORIENTED_EDGE ( 'NONE', *, *, #50327, .F. ) ;
#123747=AXIS2_PLACEMENT_3D ( 'NONE', #120516, #58933, #13912 ) ;
#123748=VERTEX_POINT ( 'NONE', #103494 ) ;
#123750=DIRECTION ( 'NONE',  ( 0.6830127018922180770, -0.6830127018922204085, -0.2588190451025213501 ) ) ;
#123751=EDGE_CURVE ( 'NONE', #79833, #43058, #136858, .T. ) ;
#123752=LINE ( 'NONE', #22945, #21810 ) ;
#123754=PLANE ( 'NONE',  #103334 ) ;
#123755=FACE_OUTER_BOUND ( 'NONE', #99359, .T. ) ;
#123757=DIRECTION ( 'NONE',  ( -0.7071067811865487940, 0.7071067811865463515, -0.000000000000000000 ) ) ;
#123758=DIRECTION ( 'NONE',  ( 0.6830127018922181881, 0.6830127018922202975, -0.2588190451025214056 ) ) ;
#123761=EDGE_CURVE ( 'NONE', #60930, #43567, #115068, .T. ) ;
#123762=VERTEX_POINT ( 'NONE', #27360 ) ;
#123764=ORIENTED_EDGE ( 'NONE', *, *, #111713, .T. ) ;
#123765=DIRECTION ( 'NONE',  ( -0.000000000000000000, 0.3543493200069153248, 0.9351131265310292928 ) ) ;
#123766=LINE ( 'NONE', #136040, #69634 ) ;
#123767=EDGE_LOOP ( 'NONE', ( #38768, #104338, #65960, #33007 ) ) ;
#123768=CARTESIAN_POINT ( 'NONE',  ( 1.603431928946415175, -14.24070752338413648, 19.24067776001726671 ) ) ;
#123769=CARTESIAN_POINT ( 'NONE',  ( -2.994519915287485734, 28.92564299267940342, 4.000000000000000000 ) ) ;
#123771=CARTESIAN_POINT ( 'NONE',  ( 6.489213562373093325, -27.52281430457059841, 5.000000000000000000 ) ) ;
#123772=ORIENTED_EDGE ( 'NONE', *, *, #80178, .F. ) ;
#123773=CARTESIAN_POINT ( 'NONE',  ( -38.99451991528749062, 28.92564299267965211, 4.000000000000000000 ) ) ;
#123774=VERTEX_POINT ( 'NONE', #60033 ) ;
#123775=VECTOR ( 'NONE', #26878, 1000.000000000000000 ) ;
#123776=LINE ( 'NONE', #24435, #38060 ) ;
#123777=ADVANCED_FACE ( 'NONE', ( #50568 ), #4867, .F. ) ;
#123782=FACE_OUTER_BOUND ( 'NONE', #122012, .T. ) ;
#123783=ORIENTED_EDGE ( 'NONE', *, *, #32951, .F. ) ;
#123784=VECTOR ( 'NONE', #11466, 1000.000000000000000 ) ;
#123785=CARTESIAN_POINT ( 'NONE',  ( 71.99451991528749772, 28.92564299267988304, 4.000000000000000000 ) ) ;
#123786=CARTESIAN_POINT ( 'NONE',  ( 62.99451991528749772, 28.92564299267982264, 4.000000000000000000 ) ) ;
#123787=CARTESIAN_POINT ( 'NONE',  ( -39.29974487139159578, -27.71228299555233576, 4.000000000000000000 ) ) ;
#123789=CARTESIAN_POINT ( 'NONE',  ( -17.99999999999987210, -9.033600742197645417, 5.000000000000000000 ) ) ;
#123790=PLANE ( 'NONE',  #130075 ) ;
#123791=DIRECTION ( 'NONE',  ( 0.7071067811865487940, 0.7071067811865463515, 0.000000000000000000 ) ) ;
#123792=ORIENTED_EDGE ( 'NONE', *, *, #50725, .T. ) ;
#123793=DIRECTION ( 'NONE',  ( 0.7071067811865487940, -0.7071067811865463515, 0.000000000000000000 ) ) ;
#123795=EDGE_CURVE ( 'NONE', #138233, #29394, #73066, .T. ) ;
#123797=DIRECTION ( 'NONE',  ( -0.7071067811865486830, -0.7071067811865464625, -0.000000000000000000 ) ) ;
#123798=DIRECTION ( 'NONE',  ( -1.000000000000000000, 0.000000000000000000, -0.000000000000000000 ) ) ;
#123799=CARTESIAN_POINT ( 'NONE',  ( -22.49999999999984013, -16.91253812416058366, 4.000000000000000000 ) ) ;
#123801=VERTEX_POINT ( 'NONE', #117219 ) ;
#123802=LINE ( 'NONE', #24457, #109949 ) ;
#123804=DIRECTION ( 'NONE',  ( -0.000000000000000000, 0.3543493200069153248, 0.9351131265310292928 ) ) ;
#123805=EDGE_LOOP ( 'NONE', ( #8243, #65845, #90016, #15805 ) ) ;
#123806=CARTESIAN_POINT ( 'NONE',  ( -30.48921356237309510, -27.52281430457076894, 5.000000000000000000 ) ) ;
#123807=EDGE_CURVE ( 'NONE', #76459, #133583, #16982, .T. ) ;
#123810=ORIENTED_EDGE ( 'NONE', *, *, #100655, .T. ) ;
#123812=LINE ( 'NONE', #77462, #19736 ) ;
#123814=PLANE ( 'NONE',  #3871 ) ;
#123815=ORIENTED_EDGE ( 'NONE', *, *, #81192, .T. ) ;
#123816=ORIENTED_EDGE ( 'NONE', *, *, #30997, .F. ) ;
#123817=EDGE_LOOP ( 'NONE', ( #79419, #77219, #141641, #93638 ) ) ;
#123819=ORIENTED_EDGE ( 'NONE', *, *, #64953, .T. ) ;
#123820=CARTESIAN_POINT ( 'NONE',  ( -36.29974487139159578, -27.71228299555231445, 4.000000000000000000 ) ) ;
#123821=EDGE_CURVE ( 'NONE', #110390, #92829, #64305, .T. ) ;
#123822=CARTESIAN_POINT ( 'NONE',  ( -8.563198967791651128, -12.74070752338415424, 9.898150129686394294 ) ) ;
#123823=EDGE_CURVE ( 'NONE', #83942, #56788, #105858, .T. ) ;
#123824=CARTESIAN_POINT ( 'NONE',  ( 26.99451991528749417, 28.92564299267956685, 4.000000000000000000 ) ) ;
#123825=LINE ( 'NONE', #58606, #61673 ) ;
#123826=ORIENTED_EDGE ( 'NONE', *, *, #83599, .F. ) ;
#123827=DIRECTION ( 'NONE',  ( -0.7071067811865486830, -0.7071067811865464625, 0.000000000000000000 ) ) ;
#123828=DIRECTION ( 'NONE',  ( -0.000000000000000000, 0.3543493200069153248, 0.9351131265310292928 ) ) ;
#123829=AXIS2_PLACEMENT_3D ( 'NONE', #13645, #78230, #113690 ) ;
#123830=CARTESIAN_POINT ( 'NONE',  ( -4.171830600776441855, 18.75929247661552424, 4.000000000000000000 ) ) ;
#123832=ORIENTED_EDGE ( 'NONE', *, *, #63992, .T. ) ;
#123833=EDGE_CURVE ( 'NONE', #7972, #100907, #23462, .T. ) ;
#123834=LINE ( 'NONE', #112234, #123026 ) ;
#123835=CARTESIAN_POINT ( 'NONE',  ( -10.25154412867569143, -11.24070752338416845, 10.39518518046011764 ) ) ;
#123836=VERTEX_POINT ( 'NONE', #981 ) ;
#123837=ORIENTED_EDGE ( 'NONE', *, *, #63335, .T. ) ;
#123838=ADVANCED_FACE ( 'NONE', ( #45265 ), #131001, .F. ) ;
#123839=DIRECTION ( 'NONE',  ( 0.6830127018922181881, 0.6830127018922202975, -0.2588190451025214056 ) ) ;
#123840=EDGE_CURVE ( 'NONE', #16613, #94289, #111166, .T. ) ;
#123845=DIRECTION ( 'NONE',  ( -0.000000000000000000, 0.000000000000000000, 1.000000000000000000 ) ) ;
#123846=DIRECTION ( 'NONE',  ( 0.7071067811865487940, 0.7071067811865463515, -0.000000000000000000 ) ) ;
#123848=VECTOR ( 'NONE', #36762, 1000.000000000000000 ) ;
#123850=ORIENTED_EDGE ( 'NONE', *, *, #95436, .F. ) ;
#123851=AXIS2_PLACEMENT_3D ( 'NONE', #39669, #126627, #6245 ) ;
#123853=ORIENTED_EDGE ( 'NONE', *, *, #13597, .T. ) ;
#123854=ORIENTED_EDGE ( 'NONE', *, *, #101167, .T. ) ;
#123856=CARTESIAN_POINT ( 'NONE',  ( 45.18398860626900415, 28.73617430169818832, 5.000000000000000000 ) ) ;
#123857=ORIENTED_EDGE ( 'NONE', *, *, #24566, .F. ) ;
#123860=CARTESIAN_POINT ( 'NONE',  ( -15.29974487139158867, -27.71228299555216879, 4.000000000000000000 ) ) ;
#123861=CARTESIAN_POINT ( 'NONE',  ( 0.000000000000000000, 21.72500000000000142, 4.500000000000000888 ) ) ;
#123862=LINE ( 'NONE', #24519, #62379 ) ;
#123864=ORIENTED_EDGE ( 'NONE', *, *, #23611, .F. ) ;
#123865=CARTESIAN_POINT ( 'NONE',  ( 51.29974487139158867, -27.71228299555242103, 4.000000000000000000 ) ) ;
#123866=EDGE_LOOP ( 'NONE', ( #105324, #28287, #66203, #69711 ) ) ;
#123868=ORIENTED_EDGE ( 'NONE', *, *, #21887, .F. ) ;
#123872=ORIENTED_EDGE ( 'NONE', *, *, #40352, .F. ) ;
#123873=EDGE_LOOP ( 'NONE', ( #19395, #46048, #134143, #31091 ) ) ;
#123875=VECTOR ( 'NONE', #18928, 1000.000000000000000 ) ;
#123878=AXIS2_PLACEMENT_3D ( 'NONE', #126698, #13649, #47088 ) ;
#123879=ADVANCED_FACE ( 'NONE', ( #11854 ), #130293, .F. ) ;
#123880=FACE_OUTER_BOUND ( 'NONE', #60655, .T. ) ;
#123882=PLANE ( 'NONE',  #135424 ) ;
#123883=VECTOR ( 'NONE', #23981, 1000.000000000000000 ) ;
#123884=EDGE_CURVE ( 'NONE', #13822, #96941, #41835, .T. ) ;
#123885=FACE_OUTER_BOUND ( 'NONE', #96598, .T. ) ;
#123886=CARTESIAN_POINT ( 'NONE',  ( 60.48921356237309510, -27.52281430457097500, 5.000000000000000000 ) ) ;
#123887=DIRECTION ( 'NONE',  ( -0.6830127018922181881, 0.6830127018922202975, -0.2588190451025214056 ) ) ;
#123888=CARTESIAN_POINT ( 'NONE',  ( -17.58838509405156003, 22.22500000000000142, 4.777194822843815025 ) ) ;
#123889=ADVANCED_FACE ( 'NONE', ( #33659 ), #86058, .F. ) ;
#123890=EDGE_CURVE ( 'NONE', #96522, #116312, #118675, .T. ) ;
#123892=VERTEX_POINT ( 'NONE', #22713 ) ;
#123893=CARTESIAN_POINT ( 'NONE',  ( -39.48921356237310221, -27.52281430457082934, 5.000000000000000000 ) ) ;
#123894=ORIENTED_EDGE ( 'NONE', *, *, #21934, .T. ) ;
#123896=CARTESIAN_POINT ( 'NONE',  ( -20.51078643762690490, -27.52281430457041012, 5.000000000000000000 ) ) ;
#123897=ORIENTED_EDGE ( 'NONE', *, *, #132872, .F. ) ;
#123898=DIRECTION ( 'NONE',  ( -0.7071067811865486830, -0.7071067811865464625, 0.000000000000000000 ) ) ;
#123899=DIRECTION ( 'NONE',  ( -0.6830127018922180770, -0.6830127018922204085, -0.2588190451025213501 ) ) ;
#123900=LINE ( 'NONE', #69525, #29383 ) ;
#123901=EDGE_CURVE ( 'NONE', #1535, #87168, #19366, .T. ) ;
#123902=DIRECTION ( 'NONE',  ( -0.000000000000000000, -0.000000000000000000, 1.000000000000000000 ) ) ;
#123904=PLANE ( 'NONE',  #58053 ) ;
#123905=ORIENTED_EDGE ( 'NONE', *, *, #29849, .T. ) ;
#123906=CARTESIAN_POINT ( 'NONE',  ( 10.04515773336659556, -21.74070752338405654, 21.72585301388586743 ) ) ;
#123907=ORIENTED_EDGE ( 'NONE', *, *, #140127, .F. ) ;
#123908=DIRECTION ( 'NONE',  ( 0.3543493200069162685, -0.000000000000000000, -0.9351131265310288487 ) ) ;
#123909=( BOUNDED_CURVE ( )  B_SPLINE_CURVE ( 3, ( #57972, #135512, #89834, #110844 ),
 .UNSPECIFIED., .F., .T. ) 
 B_SPLINE_CURVE_WITH_KNOTS ( ( 4, 4 ),
 ( 0.8834430019029044789, 0.8929338002999919199 ),
 .UNSPECIFIED. ) 
 CURVE ( )  GEOMETRIC_REPRESENTATION_ITEM ( )  RATIONAL_B_SPLINE_CURVE ( ( 1.000000000000000000, 0.9999924937429014449, 0.9999924937429014449, 1.000000000000000000 ) ) 
 REPRESENTATION_ITEM ( '' )  );
#123911=VERTEX_POINT ( 'NONE', #29509 ) ;
#123913=EDGE_CURVE ( 'NONE', #39694, #127061, #117924, .T. ) ;
#123914=PLANE ( 'NONE',  #8798 ) ;
#123915=CARTESIAN_POINT ( 'NONE',  ( -33.48921356237309510, -27.52281430457078670, 5.000000000000000000 ) ) ;
#123917=ORIENTED_EDGE ( 'NONE', *, *, #36727, .T. ) ;
#123919=CARTESIAN_POINT ( 'NONE',  ( -51.48921356237309510, -27.52281430457091460, 5.000000000000000000 ) ) ;
#123920=DIRECTION ( 'NONE',  ( 0.7071067811865487940, -0.7071067811865463515, 0.000000000000000000 ) ) ;
#123921=EDGE_CURVE ( 'NONE', #138262, #103456, #74487, .T. ) ;
#123922=LINE ( 'NONE', #24578, #8042 ) ;
#123923=DIRECTION ( 'NONE',  ( 1.000000000000000000, 0.000000000000000000, 0.000000000000000000 ) ) ;
#123924=ORIENTED_EDGE ( 'NONE', *, *, #76989, .F. ) ;
#123926=DIRECTION ( 'NONE',  ( 0.7071067811865487940, 0.7071067811865463515, 0.000000000000000000 ) ) ;
#123927=LINE ( 'NONE', #10139, #18711 ) ;
#123928=ORIENTED_EDGE ( 'NONE', *, *, #75569, .T. ) ;
#123930=PLANE ( 'NONE',  #100321 ) ;
#123931=ORIENTED_EDGE ( 'NONE', *, *, #127304, .T. ) ;
#123932=DIRECTION ( 'NONE',  ( -0.000000000000000000, 0.3543493200069153248, 0.9351131265310292928 ) ) ;
#123933=ORIENTED_EDGE ( 'NONE', *, *, #53272, .T. ) ;
#123934=VERTEX_POINT ( 'NONE', #137238 ) ;
#123935=ADVANCED_FACE ( 'NONE', ( #93011 ), #115427, .F. ) ;
#123936=CARTESIAN_POINT ( 'NONE',  ( 24.48921356237309510, -27.52281430457072631, 5.000000000000000000 ) ) ;
#123937=DIRECTION ( 'NONE',  ( -0.7071067811865486830, 0.7071067811865464625, 0.000000000000000000 ) ) ;
#123938=EDGE_CURVE ( 'NONE', #2974, #92499, #1669, .T. ) ;
#123939=ORIENTED_EDGE ( 'NONE', *, *, #38986, .T. ) ;
#123940=ORIENTED_EDGE ( 'NONE', *, *, #126033, .F. ) ;
#123941=CARTESIAN_POINT ( 'NONE',  ( -7.171830600776422315, -11.24070752338416668, 4.000000000000000000 ) ) ;
#123942=DIRECTION ( 'NONE',  ( -0.7071067811865486830, -0.7071067811865464625, 0.000000000000000000 ) ) ;
#123943=ADVANCED_FACE ( 'NONE', ( #57552 ), #81452, .F. ) ;
#123944=VECTOR ( 'NONE', #113817, 1000.000000000000227 ) ;
#123945=DIRECTION ( 'NONE',  ( -0.6830127018922180770, -0.6830127018922204085, -0.2588190451025213501 ) ) ;
#123947=VECTOR ( 'NONE', #73699, 1000.000000000000000 ) ;
#123948=FACE_OUTER_BOUND ( 'NONE', #24197, .T. ) ;
#123949=FACE_OUTER_BOUND ( 'NONE', #15032, .T. ) ;
#123950=FACE_OUTER_BOUND ( 'NONE', #9089, .T. ) ;
#123952=CARTESIAN_POINT ( 'NONE',  ( -4.001930566820951718, -22.22500000000000142, 4.500000000000000888 ) ) ;
#123953=DIRECTION ( 'NONE',  ( 1.000000000000000000, 0.000000000000000000, 0.000000000000000000 ) ) ;
#123954=CARTESIAN_POINT ( 'NONE',  ( 32.99999999999977263, -16.60178936734445543, 0.8616154019348262194 ) ) ;
#123955=DIRECTION ( 'NONE',  ( -0.7071067811865486830, -0.7071067811865464625, 0.000000000000000000 ) ) ;
#123957=EDGE_LOOP ( 'NONE', ( #142113, #95059, #18382, #13353 ) ) ;
#123959=ORIENTED_EDGE ( 'NONE', *, *, #103565, .F. ) ;
#123961=VERTEX_POINT ( 'NONE', #91584 ) ;
#123963=CARTESIAN_POINT ( 'NONE',  ( -2.510786437626908008, -27.52281430457053446, 5.000000000000000000 ) ) ;
#123964=FACE_OUTER_BOUND ( 'NONE', #131526, .T. ) ;
#123965=DIRECTION ( 'NONE',  ( -0.6830127018922181881, 0.6830127018922202975, -0.2588190451025214056 ) ) ;
#123966=VERTEX_POINT ( 'NONE', #14734 ) ;
#123967=LINE ( 'NONE', #26074, #92587 ) ;
#123968=CARTESIAN_POINT ( 'NONE',  ( 34.92499999999998295, -1.487538124160511899, 4.000000000000000000 ) ) ;
#123969=DIRECTION ( 'NONE',  ( 1.000000000000000000, 0.000000000000000000, 0.000000000000000000 ) ) ;
#123970=DIRECTION ( 'NONE',  ( 0.7071067811865487940, 0.7071067811865463515, 0.000000000000000000 ) ) ;
#123971=DIRECTION ( 'NONE',  ( -0.6830127018922180770, -0.6830127018922204085, -0.2588190451025213501 ) ) ;
#123972=DIRECTION ( 'NONE',  ( 0.7071067811865486830, -0.7071067811865464625, -0.000000000000000000 ) ) ;
#123974=CARTESIAN_POINT ( 'NONE',  ( 15.29974487139158867, -27.71228299555216879, 4.000000000000000000 ) ) ;
#123975=DIRECTION ( 'NONE',  ( 0.3543493200069162685, -0.000000000000000000, -0.9351131265310288487 ) ) ;
#123976=CARTESIAN_POINT ( 'NONE',  ( 15.18398860626900237, 28.73617430169797871, 5.000000000000000000 ) ) ;
#123979=ORIENTED_EDGE ( 'NONE', *, *, #24186, .F. ) ;
#123980=ORIENTED_EDGE ( 'NONE', *, *, #24165, .T. ) ;
#123983=VERTEX_POINT ( 'NONE', #25594 ) ;
#123984=AXIS2_PLACEMENT_3D ( 'NONE', #25382, #102973, #69654 ) ;
#123988=PLANE ( 'NONE',  #3956 ) ;
#123989=DIRECTION ( 'NONE',  ( 0.7071067811865486830, -0.7071067811865464625, -0.000000000000000000 ) ) ;
#123990=CARTESIAN_POINT ( 'NONE',  ( 8.999999999999959144, 17.58746187583906817, 4.000000000000000000 ) ) ;
#123992=VERTEX_POINT ( 'NONE', #45962 ) ;
#123993=ORIENTED_EDGE ( 'NONE', *, *, #21627, .T. ) ;
#123994=CARTESIAN_POINT ( 'NONE',  ( 60.48921356237309510, -27.52281430457097500, 5.000000000000000000 ) ) ;
#123995=CARTESIAN_POINT ( 'NONE',  ( 27.29177708983031181, -15.74070752338412049, 19.73771281079103801 ) ) ;
#123996=ORIENTED_EDGE ( 'NONE', *, *, #63333, .T. ) ;
#123997=ORIENTED_EDGE ( 'NONE', *, *, #143285, .T. ) ;
#123999=EDGE_LOOP ( 'NONE', ( #37403, #141848, #136262, #129332 ) ) ;
#124000=DIRECTION ( 'NONE',  ( 0.6830127018922180770, 0.6830127018922202975, -0.2588190451025213501 ) ) ;
#124001=EDGE_CURVE ( 'NONE', #3062, #22300, #85542, .T. ) ;
#124002=EDGE_CURVE ( 'NONE', #58222, #73971, #13995, .T. ) ;
#124004=ORIENTED_EDGE ( 'NONE', *, *, #83746, .T. ) ;
#124005=ADVANCED_FACE ( 'NONE', ( #48806 ), #24193, .F. ) ;
#124007=PLANE ( 'NONE',  #75641 ) ;
#124008=VERTEX_POINT ( 'NONE', #27030 ) ;
#124010=ORIENTED_EDGE ( 'NONE', *, *, #132450, .F. ) ;
#124012=EDGE_CURVE ( 'NONE', #128576, #137465, #35811, .T. ) ;
#124013=LINE ( 'NONE', #24680, #10423 ) ;
#124014=CARTESIAN_POINT ( 'NONE',  ( 9.183988606268997046, 28.73617430169793607, 5.000000000000000000 ) ) ;
#124015=EDGE_LOOP ( 'NONE', ( #13388, #70453, #116737, #46308 ) ) ;
#124016=FACE_OUTER_BOUND ( 'NONE', #19001, .T. ) ;
#124017=CARTESIAN_POINT ( 'NONE',  ( 0.4892135623730947680, -27.52281430457055578, 5.000000000000000000 ) ) ;
#124018=EDGE_CURVE ( 'NONE', #120303, #55061, #69872, .T. ) ;
#124019=PLANE ( 'NONE',  #28127 ) ;
#124020=FACE_BOUND ( 'NONE', #130270, .T. ) ;
#124021=ORIENTED_EDGE ( 'NONE', *, *, #105643, .F. ) ;
#124022=DIRECTION ( 'NONE',  ( -0.000000000000000000, 0.3543493200069153248, 0.9351131265310292928 ) ) ;
#124024=DIRECTION ( 'NONE',  ( -0.000000000000000000, 0.000000000000000000, 1.000000000000000000 ) ) ;
#124025=ORIENTED_EDGE ( 'NONE', *, *, #126486, .F. ) ;
#124026=DIRECTION ( 'NONE',  ( -0.6830127018922180770, -0.6830127018922204085, -0.2588190451025213501 ) ) ;
#124028=ADVANCED_FACE ( 'NONE', ( #3805 ), #134389, .T. ) ;
#124029=ORIENTED_EDGE ( 'NONE', *, *, #26664, .F. ) ;
#124030=ORIENTED_EDGE ( 'NONE', *, *, #66140, .F. ) ;
#124031=VECTOR ( 'NONE', #80951, 999.9999999999998863 ) ;
#124033=ORIENTED_EDGE ( 'NONE', *, *, #108480, .F. ) ;
#124034=CARTESIAN_POINT ( 'NONE',  ( -27.32816939922333077, 17.25929247661554200, 4.000000000000000000 ) ) ;
#124035=VECTOR ( 'NONE', #98832, 1000.000000000000227 ) ;
#124036=LINE ( 'NONE', #56684, #70560 ) ;
#124037=EDGE_CURVE ( 'NONE', #54748, #62201, #79331, .T. ) ;
#124038=ORIENTED_EDGE ( 'NONE', *, *, #142710, .T. ) ;
#124039=LINE ( 'NONE', #137780, #88496 ) ;
#124040=DIRECTION ( 'NONE',  ( 0.3543493200069162685, -0.000000000000000000, -0.9351131265310288487 ) ) ;
#124042=EDGE_CURVE ( 'NONE', #42749, #143546, #102481, .T. ) ;
#124043=LINE ( 'NONE', #100853, #16098 ) ;
#124044=DIRECTION ( 'NONE',  ( 1.000000000000000000, 0.000000000000000000, 0.000000000000000000 ) ) ;
#124046=ORIENTED_EDGE ( 'NONE', *, *, #44796, .F. ) ;
#124047=ORIENTED_EDGE ( 'NONE', *, *, #37100, .T. ) ;
#124048=ORIENTED_EDGE ( 'NONE', *, *, #12699, .T. ) ;
#124051=EDGE_CURVE ( 'NONE', #9764, #130424, #80094, .T. ) ;
#124052=ORIENTED_EDGE ( 'NONE', *, *, #119137, .T. ) ;
#124053=LINE ( 'NONE', #66122, #14256 ) ;
#124054=EDGE_CURVE ( 'NONE', #17089, #14082, #114043, .T. ) ;
#124055=CARTESIAN_POINT ( 'NONE',  ( 0.9815526536432959137, 18.75929247661553134, 20.33588619593442814 ) ) ;
#124057=LINE ( 'NONE', #60250, #44121 ) ;
#124058=EDGE_LOOP ( 'NONE', ( #112078, #51569, #57514, #136215 ) ) ;
#124059=VECTOR ( 'NONE', #91860, 1000.000000000000227 ) ;
#124060=PLANE ( 'NONE',  #93075 ) ;
#124062=VECTOR ( 'NONE', #115373, 1000.000000000000000 ) ;
#124063=CARTESIAN_POINT ( 'NONE',  ( -36.48921356237310221, -27.52281430457080802, 5.000000000000000000 ) ) ;
#124064=ORIENTED_EDGE ( 'NONE', *, *, #101005, .T. ) ;
#124066=CARTESIAN_POINT ( 'NONE',  ( 10.49999999999992362, -17.91344420646041513, 1.358650452708489054 ) ) ;
#124067=AXIS2_PLACEMENT_3D ( 'NONE', #24549, #25260, #12239 ) ;
#124068=EDGE_CURVE ( 'NONE', #129470, #119697, #129920, .T. ) ;
#124069=VECTOR ( 'NONE', #43546, 999.9999999999998863 ) ;
#124070=CARTESIAN_POINT ( 'NONE',  ( -34.42500000000001137, -22.22500000000000142, 5.000000000000000000 ) ) ;
#124071=LINE ( 'NONE', #68303, #16462 ) ;
#124072=VERTEX_POINT ( 'NONE', #94421 ) ;
#124073=DIRECTION ( 'NONE',  ( 0.7071067811865487940, -0.7071067811865463515, 0.000000000000000000 ) ) ;
#124074=FACE_OUTER_BOUND ( 'NONE', #32542, .T. ) ;
#124075=ORIENTED_EDGE ( 'NONE', *, *, #139680, .F. ) ;
#124076=DIRECTION ( 'NONE',  ( 0.3543493200069162685, -0.000000000000000000, -0.9351131265310288487 ) ) ;
#124077=VERTEX_POINT ( 'NONE', #128505 ) ;
#124078=VECTOR ( 'NONE', #84882, 1000.000000000000000 ) ;
#124079=DIRECTION ( 'NONE',  ( 0.6830127018922180770, -0.6830127018922204085, -0.2588190451025213501 ) ) ;
#124080=EDGE_CURVE ( 'NONE', #120007, #127365, #30627, .T. ) ;
#124081=CARTESIAN_POINT ( 'NONE',  ( -34.92500000000001137, -15.15525166281330627, -9.164774702225015446 ) ) ;
#124082=CARTESIAN_POINT ( 'NONE',  ( 60.48921356237309510, -27.52281430457097500, 5.000000000000000000 ) ) ;
#124083=EDGE_LOOP ( 'NONE', ( #32035, #102587, #142671, #42885 ) ) ;
#124084=CARTESIAN_POINT ( 'NONE',  ( -10.82816939922344979, -14.24070752338413293, 4.000000000000000000 ) ) ;
#124085=LINE ( 'NONE', #121209, #35235 ) ;
#124086=ORIENTED_EDGE ( 'NONE', *, *, #29923, .F. ) ;
#124087=CARTESIAN_POINT ( 'NONE',  ( 51.18398860626899705, 28.73617430169823095, 5.000000000000000000 ) ) ;
#124089=DIRECTION ( 'NONE',  ( -0.3543493200069162685, -0.000000000000000000, -0.9351131265310288487 ) ) ;
#124090=CARTESIAN_POINT ( 'NONE',  ( 34.42499999999998295, 14.97718569542923994, 5.000000000000000000 ) ) ;
#124092=ORIENTED_EDGE ( 'NONE', *, *, #101057, .F. ) ;
#124093=DIRECTION ( 'NONE',  ( -0.3543493200069162685, -0.000000000000000000, -0.9351131265310288487 ) ) ;
#124094=ORIENTED_EDGE ( 'NONE', *, *, #60290, .T. ) ;
#124095=ADVANCED_FACE ( 'NONE', ( #51659 ), #60410, .F. ) ;
#124096=EDGE_CURVE ( 'NONE', #54960, #98193, #104595, .T. ) ;
#124097=CARTESIAN_POINT ( 'NONE',  ( -45.18398860626900415, 28.73617430169818832, 5.000000000000000000 ) ) ;
#124098=EDGE_LOOP ( 'NONE', ( #135988, #126828, #64864, #140678, #266 ) ) ;
#124099=CARTESIAN_POINT ( 'NONE',  ( -15.18398860626900237, 28.73617430169797871, 5.000000000000000000 ) ) ;
#124100=DIRECTION ( 'NONE',  ( 0.7071067811865486830, -0.7071067811865464625, -0.000000000000000000 ) ) ;
#124102=FACE_OUTER_BOUND ( 'NONE', #60396, .T. ) ;
#124103=VECTOR ( 'NONE', #68700, 1000.000000000000000 ) ;
#124105=CARTESIAN_POINT ( 'NONE',  ( 17.99999999999987566, -8.731860332648819778, -2.120594902707497287 ) ) ;
#124106=ORIENTED_EDGE ( 'NONE', *, *, #35087, .T. ) ;
#124107=ORIENTED_EDGE ( 'NONE', *, *, #6436, .F. ) ;
#124108=ORIENTED_EDGE ( 'NONE', *, *, #4687, .T. ) ;
#124110=ORIENTED_EDGE ( 'NONE', *, *, #48156, .F. ) ;
#124111=ORIENTED_EDGE ( 'NONE', *, *, #43091, .T. ) ;
#124112=ORIENTED_EDGE ( 'NONE', *, *, #114876, .T. ) ;
#124114=CARTESIAN_POINT ( 'NONE',  ( -30.32816939922331656, 2.259292476615690770, 4.000000000000000000 ) ) ;
#124117=LINE ( 'NONE', #92914, #92481 ) ;
#124118=DIRECTION ( 'NONE',  ( 0.7071067811865487940, -0.7071067811865463515, 0.000000000000000000 ) ) ;
#124120=CARTESIAN_POINT ( 'NONE',  ( -2.292893218813436995, -9.740707523384184441, 5.000000000000000000 ) ) ;
#124122=VERTEX_POINT ( 'NONE', #107441 ) ;
#124123=CARTESIAN_POINT ( 'NONE',  ( 23.60898926630779826, -0.6778661889157658882, 4.000000000000000000 ) ) ;
#124124=DIRECTION ( 'NONE',  ( -0.000000000000000000, 0.3543493200069153248, 0.9351131265310292928 ) ) ;
#124126=CARTESIAN_POINT ( 'NONE',  ( 12.65494483745374588, 5.259292476615665457, 12.77922209995896807 ) ) ;
#124127=CARTESIAN_POINT ( 'NONE',  ( 23.29289321881329400, 11.25929247661560417, 5.000000000000000000 ) ) ;
#124128=CARTESIAN_POINT ( 'NONE',  ( 41.99451991528749062, 28.92564299267967343, 4.000000000000000000 ) ) ;
#124129=FACE_OUTER_BOUND ( 'NONE', #63370, .T. ) ;
#124132=DIRECTION ( 'NONE',  ( -1.000000000000000000, 0.000000000000000000, -0.000000000000000000 ) ) ;
#124133=PLANE ( 'NONE',  #80923 ) ;
#124135=EDGE_LOOP ( 'NONE', ( #82104, #15970, #12321, #89219 ) ) ;
#124137=ORIENTED_EDGE ( 'NONE', *, *, #21201, .T. ) ;
#124139=DIRECTION ( 'NONE',  ( -0.6830127018922181881, 0.6830127018922202975, -0.2588190451025214056 ) ) ;
#124140=EDGE_CURVE ( 'NONE', #8796, #98543, #50233, .T. ) ;
#124141=ORIENTED_EDGE ( 'NONE', *, *, #89242, .T. ) ;
#124143=CARTESIAN_POINT ( 'NONE',  ( 66.48921356237309510, -27.52281430457101763, 5.000000000000000000 ) ) ;
#124146=ORIENTED_EDGE ( 'NONE', *, *, #79142, .T. ) ;
#124147=LINE ( 'NONE', #49487, #45660 ) ;
#124148=ORIENTED_EDGE ( 'NONE', *, *, #54364, .T. ) ;
#124149=DIRECTION ( 'NONE',  ( 0.7071067811865487940, 0.7071067811865463515, 0.000000000000000000 ) ) ;
#124150=DIRECTION ( 'NONE',  ( 0.6830127018922180770, -0.6830127018922204085, -0.2588190451025213501 ) ) ;
#124151=CARTESIAN_POINT ( 'NONE',  ( -33.48921356237309510, -27.52281430457078670, 5.000000000000000000 ) ) ;
#124152=EDGE_CURVE ( 'NONE', #68414, #89048, #96537, .T. ) ;
#124153=CARTESIAN_POINT ( 'NONE',  ( 39.18398860626899705, 28.73617430169814568, 5.000000000000000000 ) ) ;
#124154=VERTEX_POINT ( 'NONE', #139405 ) ;
#124155=VECTOR ( 'NONE', #125231, 1000.000000000000227 ) ;
#124156=CARTESIAN_POINT ( 'NONE',  ( -42.48921356237308800, -27.52281430457085065, 5.000000000000000000 ) ) ;
#124157=EDGE_CURVE ( 'NONE', #113425, #1274, #95856, .T. ) ;
#124158=EDGE_CURVE ( 'NONE', #87398, #34254, #16882, .T. ) ;
#124159=ORIENTED_EDGE ( 'NONE', *, *, #103369, .F. ) ;
#124160=DIRECTION ( 'NONE',  ( 0.7071067811865487940, -0.7071067811865463515, 0.000000000000000000 ) ) ;
#124161=CARTESIAN_POINT ( 'NONE',  ( -14.51078643762690490, -27.52281430457045275, 5.000000000000000000 ) ) ;
#124162=LINE ( 'NONE', #37894, #63943 ) ;
#124163=CARTESIAN_POINT ( 'NONE',  ( 27.00548008471251293, 28.92564299267919381, 4.000000000000000000 ) ) ;
#124164=DIRECTION ( 'NONE',  ( -0.7071067811865486830, 0.7071067811865464625, 0.000000000000000000 ) ) ;
#124165=VECTOR ( 'NONE', #26449, 999.9999999999998863 ) ;
#124166=VECTOR ( 'NONE', #130059, 999.9999999999998863 ) ;
#124167=ADVANCED_FACE ( 'NONE', ( #61155 ), #82865, .T. ) ;
#124168=EDGE_CURVE ( 'NONE', #82994, #11548, #95135, .T. ) ;
#124170=FACE_OUTER_BOUND ( 'NONE', #121356, .T. ) ;
#124172=CARTESIAN_POINT ( 'NONE',  ( -24.99941145866615244, 2.672864951410426126, 4.679979323531659574 ) ) ;
#124173=EDGE_CURVE ( 'NONE', #47805, #46388, #8108, .T. ) ;
#124176=ORIENTED_EDGE ( 'NONE', *, *, #6927, .T. ) ;
#124179=DIRECTION ( 'NONE',  ( -0.000000000000000000, 0.3543493200069153248, 0.9351131265310292928 ) ) ;
#124180=ORIENTED_EDGE ( 'NONE', *, *, #89271, .F. ) ;
#124181=EDGE_CURVE ( 'NONE', #91814, #70943, #105303, .T. ) ;
#124183=ORIENTED_EDGE ( 'NONE', *, *, #21260, .F. ) ;
#124185=DIRECTION ( 'NONE',  ( -0.7071067811865487940, 0.7071067811865463515, -0.000000000000000000 ) ) ;
#124186=FACE_BOUND ( 'NONE', #5502, .T. ) ;
#124187=LINE ( 'NONE', #90871, #31715 ) ;
#124189=LINE ( 'NONE', #68421, #103473 ) ;
#124190=CARTESIAN_POINT ( 'NONE',  ( 81.48921356237309510, -27.52281430457112066, 5.000000000000000000 ) ) ;
#124191=CARTESIAN_POINT ( 'NONE',  ( -8.999999999999932498, -7.447814304570754551, 5.000000000000000000 ) ) ;
#124197=ORIENTED_EDGE ( 'NONE', *, *, #126830, .F. ) ;
#124198=VERTEX_POINT ( 'NONE', #63278 ) ;
#124200=EDGE_LOOP ( 'NONE', ( #101700, #37525, #93960, #27346 ) ) ;
#124201=CARTESIAN_POINT ( 'NONE',  ( -27.18398860626900060, 28.73617430169806042, 5.000000000000000000 ) ) ;
#124203=ORIENTED_EDGE ( 'NONE', *, *, #51739, .F. ) ;
#124205=VECTOR ( 'NONE', #140712, 1000.000000000000227 ) ;
#124206=CARTESIAN_POINT ( 'NONE',  ( 63.48921356237309510, -27.52281430457099631, 5.000000000000000000 ) ) ;
#124207=EDGE_CURVE ( 'NONE', #74246, #108986, #18262, .T. ) ;
#124208=CARTESIAN_POINT ( 'NONE',  ( -23.99451991528749062, 28.92564299267954908, 4.000000000000000000 ) ) ;
#124211=EDGE_CURVE ( 'NONE', #63098, #83424, #88577, .T. ) ;
#124212=LINE ( 'NONE', #48093, #91035 ) ;
#124213=CARTESIAN_POINT ( 'NONE',  ( 21.81246187583931473, -22.22500000000000142, 4.000000000000000000 ) ) ;
#124214=EDGE_LOOP ( 'NONE', ( #91793, #43458, #31143, #54471 ) ) ;
#124216=VERTEX_POINT ( 'NONE', #142247 ) ;
#124217=CARTESIAN_POINT ( 'NONE',  ( -18.63311396761903538, -2.779424156541560276, 4.000000000000000000 ) ) ;
#124218=DIRECTION ( 'NONE',  ( 0.6830127018922181881, 0.6830127018922202975, -0.2588190451025214056 ) ) ;
#124219=VERTEX_POINT ( 'NONE', #63960 ) ;
#124220=EDGE_CURVE ( 'NONE', #128218, #101990, #130658, .T. ) ;
#124222=ORIENTED_EDGE ( 'NONE', *, *, #46410, .F. ) ;
#124224=ORIENTED_EDGE ( 'NONE', *, *, #16668, .F. ) ;
#124225=LINE ( 'NONE', #55414, #13859 ) ;
#124229=CARTESIAN_POINT ( 'NONE',  ( 1.828169399223519065, -14.24070752338414358, 4.000000000000000000 ) ) ;
#124230=ORIENTED_EDGE ( 'NONE', *, *, #83000, .F. ) ;
#124231=VECTOR ( 'NONE', #11450, 1000.000000000000114 ) ;
#124232=ADVANCED_FACE ( 'NONE', ( #132810 ), #22546, .F. ) ;
#124233=FACE_OUTER_BOUND ( 'NONE', #8130, .T. ) ;
#124234=CARTESIAN_POINT ( 'NONE',  ( -17.57538274164440040, -2.608983483842240325, 5.000000000000000000 ) ) ;
#124235=FACE_OUTER_BOUND ( 'NONE', #57918, .T. ) ;
#124236=LINE ( 'NONE', #24221, #91167 ) ;
#124238=ORIENTED_EDGE ( 'NONE', *, *, #16352, .T. ) ;
#124239=FACE_OUTER_BOUND ( 'NONE', #21421, .T. ) ;
#124240=DIRECTION ( 'NONE',  ( 1.000000000000000000, 0.000000000000000000, 0.000000000000000000 ) ) ;
#124241=FACE_OUTER_BOUND ( 'NONE', #102564, .T. ) ;
#124242=ORIENTED_EDGE ( 'NONE', *, *, #78913, .T. ) ;
#124245=EDGE_CURVE ( 'NONE', #67596, #128513, #87132, .T. ) ;
#124246=VECTOR ( 'NONE', #4670, 1000.000000000000000 ) ;
#124248=CARTESIAN_POINT ( 'NONE',  ( -11.67183060077638856, 20.25929247661551003, 4.000000000000000000 ) ) ;
#124249=ORIENTED_EDGE ( 'NONE', *, *, #102605, .F. ) ;
#124250=CARTESIAN_POINT ( 'NONE',  ( 26.99999999999981171, -11.35517001088070010, -1.126524801160046607 ) ) ;
#124253=CARTESIAN_POINT ( 'NONE',  ( 17.70174076595082369, 22.22500000000000142, 24.94223936709560974 ) ) ;
#124254=VECTOR ( 'NONE', #89569, 1000.000000000000000 ) ;
#124255=LINE ( 'NONE', #134436, #110809 ) ;
#124256=ORIENTED_EDGE ( 'NONE', *, *, #58413, .F. ) ;
#124258=LINE ( 'NONE', #13333, #60995 ) ;
#124259=VECTOR ( 'NONE', #98658, 1000.000000000000000 ) ;
#124260=AXIS2_PLACEMENT_3D ( 'NONE', #53010, #40742, #61119 ) ;
#124262=CARTESIAN_POINT ( 'NONE',  ( -31.49999999999977263, 13.56627193232213102, -10.57019076586075990 ) ) ;
#124263=ADVANCED_FACE ( 'NONE', ( #89272 ), #9533, .F. ) ;
#124264=AXIS2_PLACEMENT_3D ( 'NONE', #24123, #135743, #79970 ) ;
#124265=CARTESIAN_POINT ( 'NONE',  ( -30.29974487139158867, -27.71228299555227537, 4.000000000000000000 ) ) ;
#124266=PLANE ( 'NONE',  #1989 ) ;
#124267=DIRECTION ( 'NONE',  ( -0.7071067811865487940, 0.7071067811865463515, 0.000000000000000000 ) ) ;
#124268=EDGE_CURVE ( 'NONE', #86675, #60444, #32032, .T. ) ;
#124269=ORIENTED_EDGE ( 'NONE', *, *, #126924, .F. ) ;
#124270=CARTESIAN_POINT ( 'NONE',  ( -57.48921356237308800, -27.52281430457095368, 5.000000000000000000 ) ) ;
#124274=DIRECTION ( 'NONE',  ( 0.6830127018922181881, 0.6830127018922202975, -0.2588190451025214056 ) ) ;
#124276=EDGE_CURVE ( 'NONE', #43467, #90522, #121169, .T. ) ;
#124277=LINE ( 'NONE', #110517, #67267 ) ;
#124278=ADVANCED_FACE ( 'NONE', ( #8792 ), #66806, .F. ) ;
#124279=DIRECTION ( 'NONE',  ( -0.000000000000000000, 0.3543493200069153248, 0.9351131265310292928 ) ) ;
#124280=DIRECTION ( 'NONE',  ( -0.000000000000000000, -0.3543493200069152693, 0.9351131265310292928 ) ) ;
#124281=ORIENTED_EDGE ( 'NONE', *, *, #8467, .F. ) ;
#124283=ORIENTED_EDGE ( 'NONE', *, *, #130390, .T. ) ;
#124284=LINE ( 'NONE', #91655, #19989 ) ;
#124285=DIRECTION ( 'NONE',  ( 0.7071067811865487940, 0.7071067811865463515, -0.000000000000000000 ) ) ;
#124287=DIRECTION ( 'NONE',  ( -0.7071067811865486830, 0.7071067811865464625, 0.000000000000000000 ) ) ;
#124288=EDGE_CURVE ( 'NONE', #99410, #114108, #132080, .T. ) ;
#124289=DIRECTION ( 'NONE',  ( -0.3543493200069162685, -0.000000000000000000, -0.9351131265310288487 ) ) ;
#124290=FACE_OUTER_BOUND ( 'NONE', #47872, .T. ) ;
#124292=VERTEX_POINT ( 'NONE', #20417 ) ;
#124293=DIRECTION ( 'NONE',  ( 1.000000000000000000, -0.000000000000000000, -0.000000000000000000 ) ) ;
#124294=LINE ( 'NONE', #69218, #32999 ) ;
#124296=LINE ( 'NONE', #125008, #84432 ) ;
#124298=CARTESIAN_POINT ( 'NONE',  ( -5.700255128608413102, -27.71228299555201957, 4.000000000000000000 ) ) ;
#124300=DIRECTION ( 'NONE',  ( 1.000000000000000000, 0.000000000000000000, 0.000000000000000000 ) ) ;
#124302=LINE ( 'NONE', #46060, #73771 ) ;
#124303=ORIENTED_EDGE ( 'NONE', *, *, #93232, .T. ) ;
#124305=PLANE ( 'NONE',  #142008 ) ;
#124306=LINE ( 'NONE', #101840, #20787 ) ;
#124307=LINE ( 'NONE', #46808, #70606 ) ;
#124308=VECTOR ( 'NONE', #18944, 1000.000000000000000 ) ;
#124309=ORIENTED_EDGE ( 'NONE', *, *, #101467, .T. ) ;
#124310=DIRECTION ( 'NONE',  ( -0.3543493200069162685, -0.000000000000000000, -0.9351131265310288487 ) ) ;
#124311=PLANE ( 'NONE',  #62872 ) ;
#124313=VECTOR ( 'NONE', #21047, 1000.000000000000000 ) ;
#124314=DIRECTION ( 'NONE',  ( 0.3543493200069162685, -0.000000000000000000, -0.9351131265310288487 ) ) ;
#124315=ORIENTED_EDGE ( 'NONE', *, *, #42669, .F. ) ;
#124316=ORIENTED_EDGE ( 'NONE', *, *, #106284, .F. ) ;
#124317=ADVANCED_FACE ( 'NONE', ( #43614 ), #110279, .T. ) ;
#124318=CARTESIAN_POINT ( 'NONE',  ( 26.99999999999981526, 12.83542986846999590, -1.025386466790432438 ) ) ;
#124319=FACE_OUTER_BOUND ( 'NONE', #128999, .T. ) ;
#124320=CARTESIAN_POINT ( 'NONE',  ( -17.99999999999986855, -8.151047557385087572, -8.977947279169756101 ) ) ;
#124321=DIRECTION ( 'NONE',  ( 0.6830127018922180770, -0.6830127018922204085, -0.2588190451025213501 ) ) ;
#124323=CARTESIAN_POINT ( 'NONE',  ( 66.18398860626901126, 28.73617430169833753, 5.000000000000000000 ) ) ;
#124324=ORIENTED_EDGE ( 'NONE', *, *, #96467, .T. ) ;
#124325=CARTESIAN_POINT ( 'NONE',  ( 14.67183060077636725, -9.740707523384175559, 4.000000000000000000 ) ) ;
#124326=CARTESIAN_POINT ( 'NONE',  ( 72.18398860626899705, 28.73617430169837661, 5.000000000000000000 ) ) ;
#124328=CARTESIAN_POINT ( 'NONE',  ( 39.29974487139159578, -27.71228299555233576, 4.000000000000000000 ) ) ;
#124329=ORIENTED_EDGE ( 'NONE', *, *, #40608, .F. ) ;
#124331=AXIS2_PLACEMENT_3D ( 'NONE', #58297, #91582, #135803 ) ;
#124336=EDGE_LOOP ( 'NONE', ( #79670, #100000, #19654, #98711, #25179 ) ) ;
#124338=VECTOR ( 'NONE', #45405, 1000.000000000000227 ) ;
#124339=LINE ( 'NONE', #122176, #10490 ) ;
#124340=CARTESIAN_POINT ( 'NONE',  ( -17.99999999999987566, -5.527737879153209910, -7.983877177622330734 ) ) ;
#124341=ADVANCED_FACE ( 'NONE', ( #111741 ), #80555, .T. ) ;
#124342=CARTESIAN_POINT ( 'NONE',  ( 5.816011393731002066, 28.73617430169783304, 5.000000000000000000 ) ) ;
#124343=LINE ( 'NONE', #69266, #91853 ) ;
#124344=ORIENTED_EDGE ( 'NONE', *, *, #65304, .T. ) ;
#124345=ORIENTED_EDGE ( 'NONE', *, *, #36098, .T. ) ;
#124346=ADVANCED_FACE ( 'NONE', ( #15242 ), #3637, .F. ) ;
#124347=CARTESIAN_POINT ( 'NONE',  ( -20.36090904532357015, -2.649219295539896990, 4.327832195654618630 ) ) ;
#124349=EDGE_CURVE ( 'NONE', #57164, #2746, #69691, .T. ) ;
#124350=ORIENTED_EDGE ( 'NONE', *, *, #33227, .T. ) ;
#124351=CARTESIAN_POINT ( 'NONE',  ( -29.29289321881324426, 2.259292476615688994, 5.000000000000000000 ) ) ;
#124352=ORIENTED_EDGE ( 'NONE', *, *, #25896, .F. ) ;
#124353=CARTESIAN_POINT ( 'NONE',  ( 17.99451991528748351, 28.92564299267950645, 4.000000000000000000 ) ) ;
#124354=PLANE ( 'NONE',  #121173 ) ;
#124355=ORIENTED_EDGE ( 'NONE', *, *, #142233, .F. ) ;
#124356=ADVANCED_FACE ( 'NONE', ( #67545 ), #46531, .T. ) ;
#124358=FACE_BOUND ( 'NONE', #64369, .T. ) ;
#124359=CARTESIAN_POINT ( 'NONE',  ( 28.17183060077627843, -11.24070752338417201, 4.000000000000000000 ) ) ;
#124360=FACE_OUTER_BOUND ( 'NONE', #45782, .T. ) ;
#124361=DIRECTION ( 'NONE',  ( -0.000000000000000000, 0.000000000000000000, 1.000000000000000000 ) ) ;
#124362=CARTESIAN_POINT ( 'NONE',  ( 9.489213562373095101, -27.52281430457062328, 5.000000000000000000 ) ) ;
#124363=EDGE_CURVE ( 'NONE', #56202, #12987, #113870, .T. ) ;
#124364=AXIS2_PLACEMENT_3D ( 'NONE', #123505, #67704, #21999 ) ;
#124365=AXIS2_PLACEMENT_3D ( 'NONE', #142036, #12198, #67323 ) ;
#124366=DIRECTION ( 'NONE',  ( -0.7071067811865486830, -0.7071067811865464625, -0.000000000000000000 ) ) ;
#124368=ORIENTED_EDGE ( 'NONE', *, *, #72059, .T. ) ;
#124369=AXIS2_PLACEMENT_3D ( 'NONE', #43556, #87778, #12343 ) ;
#124370=ORIENTED_EDGE ( 'NONE', *, *, #16713, .T. ) ;
#124373=DIRECTION ( 'NONE',  ( -0.7071067811865487940, 0.7071067811865463515, 0.000000000000000000 ) ) ;
#124374=ORIENTED_EDGE ( 'NONE', *, *, #45865, .F. ) ;
#124375=VECTOR ( 'NONE', #53160, 1000.000000000000000 ) ;
#124376=DIRECTION ( 'NONE',  ( -0.7071067811865487940, 0.7071067811865463515, -0.000000000000000000 ) ) ;
#124378=DIRECTION ( 'NONE',  ( -0.3543493200069162685, -0.000000000000000000, -0.9351131265310288487 ) ) ;
#124379=ORIENTED_EDGE ( 'NONE', *, *, #77335, .F. ) ;
#124381=CARTESIAN_POINT ( 'NONE',  ( 2.999999999999975131, 10.93112307739207267, 4.000000000000000000 ) ) ;
#124382=LINE ( 'NONE', #35268, #79836 ) ;
#124383=EDGE_CURVE ( 'NONE', #22013, #68609, #110516, .T. ) ;
#124384=CARTESIAN_POINT ( 'NONE',  ( 16.83455439249994612, 8.717631302929021331, 5.000000000000000000 ) ) ;
#124385=CARTESIAN_POINT ( 'NONE',  ( 26.99999999999981526, -10.77435723561691994, -9.972017380717289825 ) ) ;
#124387=LINE ( 'NONE', #82328, #79692 ) ;
#124388=EDGE_CURVE ( 'NONE', #116079, #98487, #47254, .T. ) ;
#124389=DIRECTION ( 'NONE',  ( -0.7071067811865486830, 0.7071067811865464625, 0.000000000000000000 ) ) ;
#124390=VERTEX_POINT ( 'NONE', #59521 ) ;
#124391=ORIENTED_EDGE ( 'NONE', *, *, #30946, .F. ) ;
#124392=ORIENTED_EDGE ( 'NONE', *, *, #135644, .T. ) ;
#124394=VECTOR ( 'NONE', #80057, 1000.000000000000227 ) ;
#124395=ORIENTED_EDGE ( 'NONE', *, *, #115823, .T. ) ;
#124396=EDGE_CURVE ( 'NONE', #107388, #22970, #103677, .T. ) ;
#124397=AXIS2_PLACEMENT_3D ( 'NONE', #1378, #80424, #25288 ) ;
#124400=CARTESIAN_POINT ( 'NONE',  ( -1.499999999999990896, 19.39370406404967184, 1.459788787078205141 ) ) ;
#124403=CARTESIAN_POINT ( 'NONE',  ( -17.51078643762690845, -27.52281430457043143, 5.000000000000000000 ) ) ;
#124406=DIRECTION ( 'NONE',  ( 0.7071067811865487940, -0.7071067811865463515, 0.000000000000000000 ) ) ;
#124407=ORIENTED_EDGE ( 'NONE', *, *, #133262, .F. ) ;
#124408=DIRECTION ( 'NONE',  ( 0.7071067811865486830, -0.7071067811865464625, -0.000000000000000000 ) ) ;
#124409=LINE ( 'NONE', #103348, #66868 ) ;
#124412=LINE ( 'NONE', #44764, #75834 ) ;
#124413=EDGE_LOOP ( 'NONE', ( #126987, #101999, #71913, #29183 ) ) ;
#124414=ORIENTED_EDGE ( 'NONE', *, *, #49900, .T. ) ;
#124415=EDGE_LOOP ( 'NONE', ( #31048, #112980, #14663, #142537 ) ) ;
#124416=LINE ( 'NONE', #48280, #132724 ) ;
#124417=VECTOR ( 'NONE', #122497, 1000.000000000000000 ) ;
#124418=DIRECTION ( 'NONE',  ( 0.6830127018922180770, -0.6830127018922204085, -0.2588190451025213501 ) ) ;
#124419=DIRECTION ( 'NONE',  ( 0.6830127018922181881, 0.6830127018922202975, -0.2588190451025214056 ) ) ;
#124420=EDGE_CURVE ( 'NONE', #44265, #45274, #123349, .T. ) ;
#124421=CARTESIAN_POINT ( 'NONE',  ( -34.92500000000001137, 22.22500000000000142, 0.4999999999999995559 ) ) ;
#124422=EDGE_CURVE ( 'NONE', #13073, #89747, #4320, .T. ) ;
#124423=FACE_OUTER_BOUND ( 'NONE', #140565, .T. ) ;
#124424=EDGE_LOOP ( 'NONE', ( #49947, #12066, #40375, #22299 ) ) ;
#124426=DIRECTION ( 'NONE',  ( 0.6830127018922180770, -0.6830127018922204085, -0.2588190451025213501 ) ) ;
#124427=CARTESIAN_POINT ( 'NONE',  ( -78.18398860626899705, 28.73617430169841924, 5.000000000000000000 ) ) ;
#124429=CARTESIAN_POINT ( 'NONE',  ( 2.384059369432880882, 22.22500000000000142, -9.137797280955542334 ) ) ;
#124430=VERTEX_POINT ( 'NONE', #2956 ) ;
#124431=EDGE_LOOP ( 'NONE', ( #135051, #92603, #57289, #31677 ) ) ;
#124432=ORIENTED_EDGE ( 'NONE', *, *, #120353, .F. ) ;
#124436=DIRECTION ( 'NONE',  ( -1.000000000000000000, 0.000000000000000000, 0.000000000000000000 ) ) ;
#124437=DIRECTION ( 'NONE',  ( 0.7071067811865487940, -0.7071067811865463515, 0.000000000000000000 ) ) ;
#124438=EDGE_CURVE ( 'NONE', #68957, #115494, #135637, .T. ) ;
#124439=CARTESIAN_POINT ( 'NONE',  ( 33.32816939922330590, 14.25929247661557397, 4.000000000000000000 ) ) ;
#124440=ADVANCED_FACE ( 'NONE', ( #94953 ), #94252, .F. ) ;
#124441=LINE ( 'NONE', #44795, #15886 ) ;
#124442=VECTOR ( 'NONE', #41558, 1000.000000000000000 ) ;
#124443=EDGE_CURVE ( 'NONE', #128263, #3015, #20766, .T. ) ;
#124444=CARTESIAN_POINT ( 'NONE',  ( 21.16809626817622103, 8.755558144015518351, 4.000000000000000000 ) ) ;
#124445=DIRECTION ( 'NONE',  ( -0.6830127018922180770, -0.6830127018922204085, -0.2588190451025213501 ) ) ;
#124446=LINE ( 'NONE', #40157, #134561 ) ;
#124447=CARTESIAN_POINT ( 'NONE',  ( 1.499999999999990896, -14.56887692260766443, 4.000000000000000000 ) ) ;
#124448=ORIENTED_EDGE ( 'NONE', *, *, #18437, .F. ) ;
#124450=ORIENTED_EDGE ( 'NONE', *, *, #83488, .F. ) ;
#124451=AXIS2_PLACEMENT_3D ( 'NONE', #38296, #29529, #73772 ) ;
#124452=CARTESIAN_POINT ( 'NONE',  ( -34.49999999999975842, 5.696342897626469615, -7.587980461218476691 ) ) ;
#124453=DIRECTION ( 'NONE',  ( -0.000000000000000000, -0.3543493200069152693, 0.9351131265310292928 ) ) ;
#124454=EDGE_LOOP ( 'NONE', ( #52533, #132719, #31881, #86061 ) ) ;
#124456=ADVANCED_FACE ( 'NONE', ( #39174 ), #127615, .F. ) ;
#124458=CARTESIAN_POINT ( 'NONE',  ( 20.99999999999985434, 10.55218569542906160, 5.000000000000000000 ) ) ;
#124460=ORIENTED_EDGE ( 'NONE', *, *, #117277, .F. ) ;
#124461=CARTESIAN_POINT ( 'NONE',  ( -15.29974487139158867, -27.71228299555216879, 4.000000000000000000 ) ) ;
#124462=ORIENTED_EDGE ( 'NONE', *, *, #61428, .T. ) ;
#124463=LINE ( 'NONE', #67993, #35165 ) ;
#124467=LINE ( 'NONE', #71531, #7900 ) ;
#124468=VECTOR ( 'NONE', #47189, 1000.000000000000227 ) ;
#124470=CARTESIAN_POINT ( 'NONE',  ( 26.99999999999981881, 13.55218569542903317, 5.000000000000000000 ) ) ;
#124471=ORIENTED_EDGE ( 'NONE', *, *, #54560, .T. ) ;
#124472=CARTESIAN_POINT ( 'NONE',  ( -41.99451991528749062, 28.92564299267967343, 4.000000000000000000 ) ) ;
#124473=DIRECTION ( 'NONE',  ( -0.3543493200069162685, -0.000000000000000000, -0.9351131265310288487 ) ) ;
#124474=LINE ( 'NONE', #12834, #18280 ) ;
#124477=AXIS2_PLACEMENT_3D ( 'NONE', #52651, #67866, #111307 ) ;
#124480=EDGE_LOOP ( 'NONE', ( #107960, #99277, #55451, #27959 ) ) ;
#124481=CARTESIAN_POINT ( 'NONE',  ( -19.95484226663321436, -21.74070752338405299, 21.72585301388579992 ) ) ;
#124482=ORIENTED_EDGE ( 'NONE', *, *, #62977, .T. ) ;
#124485=LINE ( 'NONE', #14293, #55564 ) ;
#124486=EDGE_CURVE ( 'NONE', #141655, #100403, #118119, .T. ) ;
#124487=DIRECTION ( 'NONE',  ( -0.7071067811865486830, 0.7071067811865464625, 0.000000000000000000 ) ) ;
#124489=VERTEX_POINT ( 'NONE', #18827 ) ;
#124490=CARTESIAN_POINT ( 'NONE',  ( -34.82816939922328459, -14.24070752338413826, 4.000000000000000000 ) ) ;
#124491=LINE ( 'NONE', #111469, #76670 ) ;
#124492=ORIENTED_EDGE ( 'NONE', *, *, #109132, .F. ) ;
#124493=CARTESIAN_POINT ( 'NONE',  ( -30.18398860626900060, 28.73617430169808173, 5.000000000000000000 ) ) ;
#124494=CARTESIAN_POINT ( 'NONE',  ( -17.51078643762690845, -27.52281430457043143, 5.000000000000000000 ) ) ;
#124495=PLANE ( 'NONE',  #121529 ) ;
#124496=ORIENTED_EDGE ( 'NONE', *, *, #137597, .F. ) ;
#124497=FACE_OUTER_BOUND ( 'NONE', #105702, .T. ) ;
#124498=VECTOR ( 'NONE', #77351, 1000.000000000000000 ) ;
#124500=CARTESIAN_POINT ( 'NONE',  ( 0.2416945842518697374, 0.7592924766157104211, 14.37146558664982621 ) ) ;
#124502=DIRECTION ( 'NONE',  ( -0.6830127018922180770, -0.6830127018922204085, -0.2588190451025213501 ) ) ;
#124503=ORIENTED_EDGE ( 'NONE', *, *, #35943, .T. ) ;
#124505=ORIENTED_EDGE ( 'NONE', *, *, #92507, .T. ) ;
#124506=EDGE_CURVE ( 'NONE', #127352, #17335, #7214, .T. ) ;
#124509=VERTEX_POINT ( 'NONE', #63096 ) ;
#124510=ADVANCED_FACE ( 'NONE', ( #7943 ), #107266, .F. ) ;
#124511=EDGE_CURVE ( 'NONE', #54378, #33777, #39917, .T. ) ;
#124512=CARTESIAN_POINT ( 'NONE',  ( -11.99999999999991651, 8.966399257802171618, 5.000000000000000000 ) ) ;
#124513=CARTESIAN_POINT ( 'NONE',  ( -11.39513766812472184, 21.75929247661549937, 21.32995629748188904 ) ) ;
#124514=EDGE_CURVE ( 'NONE', #3029, #53162, #61661, .T. ) ;
#124515=CARTESIAN_POINT ( 'NONE',  ( 20.99999999999985789, -12.03360074219761344, 5.000000000000000000 ) ) ;
#124516=DIRECTION ( 'NONE',  ( -0.7071067811865487940, 0.7071067811865463515, 0.000000000000000000 ) ) ;
#124517=EDGE_LOOP ( 'NONE', ( #22096, #90264, #125109, #92113 ) ) ;
#124518=EDGE_CURVE ( 'NONE', #12215, #68587, #26857, .T. ) ;
#124519=CARTESIAN_POINT ( 'NONE',  ( 14.24715658456393541, 6.719242673238161601, 5.000000000000000000 ) ) ;
#124520=DIRECTION ( 'NONE',  ( -0.000000000000000000, 0.3543493200069153248, 0.9351131265310292928 ) ) ;
#124522=CARTESIAN_POINT ( 'NONE',  ( 27.98911971346032246, -22.02621442084248216, 4.990779571109221990 ) ) ;
#124524=VERTEX_POINT ( 'NONE', #95679 ) ;
#124525=EDGE_CURVE ( 'NONE', #16309, #99319, #60232, .T. ) ;
#124526=FACE_OUTER_BOUND ( 'NONE', #50198, .T. ) ;
#124527=CARTESIAN_POINT ( 'NONE',  ( -10.73248902172657360, 22.22500000000000142, -4.167446773218399514 ) ) ;
#124528=LINE ( 'NONE', #46290, #53962 ) ;
#124529=EDGE_LOOP ( 'NONE', ( #61024, #100462, #62903, #34506 ) ) ;
#124530=VERTEX_POINT ( 'NONE', #84136 ) ;
#124531=EDGE_CURVE ( 'NONE', #70558, #129671, #138492, .T. ) ;
#124532=DIRECTION ( 'NONE',  ( 0.7071067811865486830, -0.7071067811865464625, -0.000000000000000000 ) ) ;
#124533=EDGE_CURVE ( 'NONE', #18734, #7814, #16696, .T. ) ;
#124534=DIRECTION ( 'NONE',  ( 0.7071067811865487940, 0.7071067811865463515, -0.000000000000000000 ) ) ;
#124536=CARTESIAN_POINT ( 'NONE',  ( 56.99451991528749062, 28.92564299267978001, 4.000000000000000000 ) ) ;
#124538=ADVANCED_FACE ( 'NONE', ( #60975 ), #38460, .F. ) ;
#124540=CARTESIAN_POINT ( 'NONE',  ( -3.299744871391591339, -27.71228299555208352, 4.000000000000000000 ) ) ;
#124541=ORIENTED_EDGE ( 'NONE', *, *, #129548, .F. ) ;
#124543=EDGE_LOOP ( 'NONE', ( #20703, #3508, #63500, #19083 ) ) ;
#124545=ORIENTED_EDGE ( 'NONE', *, *, #127048, .F. ) ;
#124546=ORIENTED_EDGE ( 'NONE', *, *, #106448, .F. ) ;
#124547=AXIS2_PLACEMENT_3D ( 'NONE', #26255, #70518, #15331 ) ;
#124548=DIRECTION ( 'NONE',  ( 1.000000000000000000, 0.000000000000000000, 0.000000000000000000 ) ) ;
#124549=ORIENTED_EDGE ( 'NONE', *, *, #133702, .F. ) ;
#124551=CARTESIAN_POINT ( 'NONE',  ( -4.001930566820951718, -22.22500000000000142, 4.500000000000000888 ) ) ;
#124552=EDGE_CURVE ( 'NONE', #136197, #88472, #50060, .T. ) ;
#124553=CARTESIAN_POINT ( 'NONE',  ( 7.499999999999951150, 7.466399257802184053, 5.000000000000000000 ) ) ;
#124554=AXIS2_PLACEMENT_3D ( 'NONE', #64885, #109066, #98219 ) ;
#124555=DIRECTION ( 'NONE',  ( 0.7071067811865486830, -0.7071067811865464625, -0.000000000000000000 ) ) ;
#124556=ORIENTED_EDGE ( 'NONE', *, *, #135676, .T. ) ;
#124557=CARTESIAN_POINT ( 'NONE',  ( -34.92500000000001137, 15.66246187583883831, 4.000000000000000000 ) ) ;
#124558=VECTOR ( 'NONE', #48786, 1000.000000000000000 ) ;
#124559=VERTEX_POINT ( 'NONE', #73243 ) ;
#124560=CARTESIAN_POINT ( 'NONE',  ( -5.207106781186503497, 12.75929247661559351, 5.000000000000000000 ) ) ;
#124561=ORIENTED_EDGE ( 'NONE', *, *, #63935, .F. ) ;
#124562=ORIENTED_EDGE ( 'NONE', *, *, #62969, .T. ) ;
#124563=DIRECTION ( 'NONE',  ( -0.000000000000000000, 0.3543493200069153248, 0.9351131265310292928 ) ) ;
#124565=ORIENTED_EDGE ( 'NONE', *, *, #90436, .T. ) ;
#124566=FACE_OUTER_BOUND ( 'NONE', #19497, .T. ) ;
#124567=VECTOR ( 'NONE', #129186, 999.9999999999998863 ) ;
#124569=VECTOR ( 'NONE', #62176, 1000.000000000000000 ) ;
#124571=LINE ( 'NONE', #114400, #25746 ) ;
#124572=PLANE ( 'NONE',  #40277 ) ;
#124574=DIRECTION ( 'NONE',  ( 1.000000000000000000, 0.000000000000000000, 0.000000000000000000 ) ) ;
#124575=EDGE_CURVE ( 'NONE', #44742, #81070, #106531, .T. ) ;
#124577=LINE ( 'NONE', #57931, #21224 ) ;
#124579=LINE ( 'NONE', #4151, #42430 ) ;
#124581=ORIENTED_EDGE ( 'NONE', *, *, #10478, .F. ) ;
#124582=CARTESIAN_POINT ( 'NONE',  ( 0.000000000000000000, 0.000000000000000000, 5.000000000000000000 ) ) ;
#124583=CARTESIAN_POINT ( 'NONE',  ( -39.48921356237310221, -27.52281430457082934, 5.000000000000000000 ) ) ;
#124584=ADVANCED_FACE ( 'NONE', ( #66643 ), #97064, .F. ) ;
#124586=ORIENTED_EDGE ( 'NONE', *, *, #31781, .F. ) ;
#124587=CARTESIAN_POINT ( 'NONE',  ( -26.29289321881326913, -12.74070752338415602, 5.000000000000000000 ) ) ;
#124589=VECTOR ( 'NONE', #82223, 1000.000000000000227 ) ;
#124590=DIRECTION ( 'NONE',  ( -0.000000000000000000, 0.000000000000000000, 1.000000000000000000 ) ) ;
#124592=EDGE_CURVE ( 'NONE', #105871, #92747, #9349, .T. ) ;
#124593=LINE ( 'NONE', #81110, #54187 ) ;
#124594=CARTESIAN_POINT ( 'NONE',  ( -22.55363393633058067, -22.22500000000000142, 0.3120269325270338401 ) ) ;
#124595=EDGE_LOOP ( 'NONE', ( #17971, #107862, #18188, #137570 ) ) ;
#124597=LINE ( 'NONE', #134793, #74340 ) ;
#124599=LINE ( 'NONE', #2061, #2818 ) ;
#124601=VERTEX_POINT ( 'NONE', #99226 ) ;
#124603=DIRECTION ( 'NONE',  ( -0.7071067811865486830, 0.7071067811865464625, 0.000000000000000000 ) ) ;
#124604=EDGE_LOOP ( 'NONE', ( #107730, #124391, #82586, #11495 ) ) ;
#124605=VERTEX_POINT ( 'NONE', #141329 ) ;
#124606=ORIENTED_EDGE ( 'NONE', *, *, #95271, .F. ) ;
#124607=PLANE ( 'NONE',  #31075 ) ;
#124608=DIRECTION ( 'NONE',  ( 0.6830127018922180770, -0.6830127018922204085, -0.2588190451025213501 ) ) ;
#124609=CARTESIAN_POINT ( 'NONE',  ( -2.207106781186527922, 15.75929247661555443, 5.000000000000000000 ) ) ;
#124610=VECTOR ( 'NONE', #47083, 1000.000000000000000 ) ;
#124611=PLANE ( 'NONE',  #26467 ) ;
#124612=ORIENTED_EDGE ( 'NONE', *, *, #101761, .F. ) ;
#124613=CARTESIAN_POINT ( 'NONE',  ( 8.999999999999925393, -10.77435723561694836, -9.972017380717252522 ) ) ;
#124614=AXIS2_PLACEMENT_3D ( 'NONE', #114111, #135869, #36549 ) ;
#124615=EDGE_CURVE ( 'NONE', #39763, #135646, #31166, .T. ) ;
#124616=DIRECTION ( 'NONE',  ( 0.7071067811865487940, 0.7071067811865463515, -0.000000000000000000 ) ) ;
#124617=EDGE_CURVE ( 'NONE', #77841, #29516, #54365, .T. ) ;
#124618=LINE ( 'NONE', #5666, #139449 ) ;
#124619=ORIENTED_EDGE ( 'NONE', *, *, #88689, .F. ) ;
#124622=EDGE_CURVE ( 'NONE', #10035, #7970, #20437, .T. ) ;
#124624=ORIENTED_EDGE ( 'NONE', *, *, #38903, .T. ) ;
#124625=ORIENTED_EDGE ( 'NONE', *, *, #68172, .F. ) ;
#124626=EDGE_CURVE ( 'NONE', #78422, #98176, #53628, .T. ) ;
#124627=CARTESIAN_POINT ( 'NONE',  ( -4.499999999999968914, -10.04351517176479014, -1.623559851933833453 ) ) ;
#124628=DIRECTION ( 'NONE',  ( -0.000000000000000000, 0.3543493200069153248, 0.9351131265310292928 ) ) ;
#124629=VERTEX_POINT ( 'NONE', #32593 ) ;
#124630=DIRECTION ( 'NONE',  ( -0.7071067811865487940, 0.7071067811865463515, 0.000000000000000000 ) ) ;
#124632=VERTEX_POINT ( 'NONE', #120249 ) ;
#124633=CARTESIAN_POINT ( 'NONE',  ( -20.29289321881331531, 11.25929247661560062, 5.000000000000000000 ) ) ;
#124634=CARTESIAN_POINT ( 'NONE',  ( 1.499999999999989120, 21.43112307739196964, 4.000000000000000000 ) ) ;
#124635=CARTESIAN_POINT ( 'NONE',  ( 25.19018167574432709, -18.74070752338409562, 7.910009926591448526 ) ) ;
#124636=VECTOR ( 'NONE', #125654, 1000.000000000000000 ) ;
#124637=CARTESIAN_POINT ( 'NONE',  ( -28.17183060077627843, -5.240707523384232402, 4.000000000000000000 ) ) ;
#124638=CARTESIAN_POINT ( 'NONE',  ( -16.17183060077634948, -17.24070752338410273, 4.000000000000000000 ) ) ;
#124640=LINE ( 'NONE', #102193, #44923 ) ;
#124643=LINE ( 'NONE', #113768, #132527 ) ;
#124644=DIRECTION ( 'NONE',  ( -0.7071067811865487940, 0.7071067811865463515, -0.000000000000000000 ) ) ;
#124645=DIRECTION ( 'NONE',  ( 0.3543493200069164351, -0.000000000000000000, -0.9351131265310288487 ) ) ;
#124646=LINE ( 'NONE', #70322, #59428 ) ;
#124648=ADVANCED_FACE ( 'NONE', ( #75376 ), #142076, .F. ) ;
#124649=VERTEX_POINT ( 'NONE', #129736 ) ;
#124651=ORIENTED_EDGE ( 'NONE', *, *, #9452, .F. ) ;
#124652=ORIENTED_EDGE ( 'NONE', *, *, #142496, .T. ) ;
#124653=VECTOR ( 'NONE', #139261, 1000.000000000000000 ) ;
#124654=ORIENTED_EDGE ( 'NONE', *, *, #37954, .F. ) ;
#124655=DIRECTION ( 'NONE',  ( -0.7071067811865487940, 0.7071067811865463515, 0.000000000000000000 ) ) ;
#124656=DIRECTION ( 'NONE',  ( -0.000000000000000000, 0.000000000000000000, 1.000000000000000000 ) ) ;
#124658=ORIENTED_EDGE ( 'NONE', *, *, #10873, .T. ) ;
#124660=VECTOR ( 'NONE', #91618, 1000.000000000000114 ) ;
#124661=PLANE ( 'NONE',  #118022 ) ;
#124662=PLANE ( 'NONE',  #46527 ) ;
#124663=AXIS2_PLACEMENT_3D ( 'NONE', #140748, #137390, #118279 ) ;
#124664=DIRECTION ( 'NONE',  ( 1.000000000000000000, 0.000000000000000000, 0.000000000000000000 ) ) ;
#124666=VECTOR ( 'NONE', #31724, 1000.000000000000000 ) ;
#124668=LINE ( 'NONE', #64766, #114143 ) ;
#124670=VECTOR ( 'NONE', #72566, 1000.000000000000227 ) ;
#124672=CARTESIAN_POINT ( 'NONE',  ( 24.98358986394466186, 3.827854121229848694, 4.315828149752546139 ) ) ;
#124673=LINE ( 'NONE', #123276, #87019 ) ;
#124674=AXIS2_PLACEMENT_3D ( 'NONE', #31381, #110333, #65464 ) ;
#124675=LINE ( 'NONE', #10879, #10521 ) ;
#124676=VERTEX_POINT ( 'NONE', #109418 ) ;
#124677=ORIENTED_EDGE ( 'NONE', *, *, #131863, .T. ) ;
#124678=EDGE_CURVE ( 'NONE', #68424, #86982, #131171, .T. ) ;
#124681=ORIENTED_EDGE ( 'NONE', *, *, #89484, .F. ) ;
#124682=ADVANCED_FACE ( 'NONE', ( #42765 ), #76085, .F. ) ;
#124685=CARTESIAN_POINT ( 'NONE',  ( 29.99451991528749417, 28.92564299267958816, 4.000000000000000000 ) ) ;
#124686=EDGE_CURVE ( 'NONE', #71456, #68931, #65957, .T. ) ;
#124689=CARTESIAN_POINT ( 'NONE',  ( -19.82816939922339117, 15.75929247661555799, 4.000000000000000000 ) ) ;
#124690=AXIS2_PLACEMENT_3D ( 'NONE', #47670, #113578, #67242 ) ;
#124692=EDGE_LOOP ( 'NONE', ( #78403, #77579, #41367, #120576 ) ) ;
#124693=ORIENTED_EDGE ( 'NONE', *, *, #107591, .T. ) ;
#124694=DIRECTION ( 'NONE',  ( 0.7071067811865486830, -0.7071067811865464625, -0.000000000000000000 ) ) ;
#124695=CARTESIAN_POINT ( 'NONE',  ( -34.11017322888186953, -22.22500000000000497, 4.785647885939355639 ) ) ;
#124697=ORIENTED_EDGE ( 'NONE', *, *, #101078, .T. ) ;
#124698=ORIENTED_EDGE ( 'NONE', *, *, #1564, .F. ) ;
#124699=ADVANCED_FACE ( 'NONE', ( #130480 ), #55058, .F. ) ;
#124700=VERTEX_POINT ( 'NONE', #52869 ) ;
#124701=PLANE ( 'NONE',  #120895 ) ;
#124702=EDGE_CURVE ( 'NONE', #71690, #114228, #132643, .T. ) ;
#124704=VECTOR ( 'NONE', #49257, 999.9999999999998863 ) ;
#124706=EDGE_LOOP ( 'NONE', ( #28146, #114542, #63069, #94470 ) ) ;
#124707=ORIENTED_EDGE ( 'NONE', *, *, #95185, .F. ) ;
#124708=DIRECTION ( 'NONE',  ( -0.6830127018922180770, -0.6830127018922204085, -0.2588190451025213501 ) ) ;
#124709=EDGE_LOOP ( 'NONE', ( #621, #96009, #73385, #4305 ) ) ;
#124710=EDGE_LOOP ( 'NONE', ( #39349, #43067, #65414, #94342 ) ) ;
#124711=EDGE_CURVE ( 'NONE', #29397, #113191, #19550, .T. ) ;
#124713=VECTOR ( 'NONE', #95921, 999.9999999999998863 ) ;
#124714=CARTESIAN_POINT ( 'NONE',  ( -59.99451991528749772, 28.92564299267980132, 4.000000000000000000 ) ) ;
#124715=FACE_OUTER_BOUND ( 'NONE', #21849, .T. ) ;
#124717=EDGE_LOOP ( 'NONE', ( #46922, #25587, #24198, #8839 ) ) ;
#124718=LINE ( 'NONE', #23237, #32146 ) ;
#124719=CARTESIAN_POINT ( 'NONE',  ( -20.20710678118640402, -8.240707523384189770, 5.000000000000000000 ) ) ;
#124720=ADVANCED_FACE ( 'NONE', ( #20247 ), #78968, .F. ) ;
#124721=DIRECTION ( 'NONE',  ( -0.000000000000000000, 0.000000000000000000, 1.000000000000000000 ) ) ;
#124723=FACE_BOUND ( 'NONE', #119675, .T. ) ;
#124726=DIRECTION ( 'NONE',  ( -0.000000000000000000, 0.000000000000000000, 1.000000000000000000 ) ) ;
#124728=ORIENTED_EDGE ( 'NONE', *, *, #58641, .F. ) ;
#124730=DIRECTION ( 'NONE',  ( 0.6830127018922180770, -0.6830127018922204085, -0.2588190451025213501 ) ) ;
#124731=ORIENTED_EDGE ( 'NONE', *, *, #123371, .F. ) ;
#124732=EDGE_CURVE ( 'NONE', #126893, #10073, #14394, .T. ) ;
#124733=ORIENTED_EDGE ( 'NONE', *, *, #83908, .T. ) ;
#124735=EDGE_CURVE ( 'NONE', #69740, #113816, #58675, .T. ) ;
#124737=ORIENTED_EDGE ( 'NONE', *, *, #65546, .F. ) ;
#124738=DIRECTION ( 'NONE',  ( 0.6830127018922180770, -0.6830127018922204085, -0.2588190451025213501 ) ) ;
#124739=PLANE ( 'NONE',  #99269 ) ;
#124741=VERTEX_POINT ( 'NONE', #25991 ) ;
#124744=CARTESIAN_POINT ( 'NONE',  ( 34.92499999999998295, -6.048682586364314773, 15.71395525773010604 ) ) ;
#124746=CARTESIAN_POINT ( 'NONE',  ( 45.48921356237309510, -27.52281430457087197, 5.000000000000000000 ) ) ;
#124747=DIRECTION ( 'NONE',  ( -0.000000000000000000, 0.000000000000000000, 1.000000000000000000 ) ) ;
#124748=CARTESIAN_POINT ( 'NONE',  ( -10.17183060077639389, 18.75929247661552424, 4.000000000000000000 ) ) ;
#124750=ORIENTED_EDGE ( 'NONE', *, *, #72823, .F. ) ;
#124752=ORIENTED_EDGE ( 'NONE', *, *, #50119, .F. ) ;
#124753=LINE ( 'NONE', #48631, #51851 ) ;
#124756=ORIENTED_EDGE ( 'NONE', *, *, #37600, .F. ) ;
#124757=VECTOR ( 'NONE', #52839, 1000.000000000000000 ) ;
#124758=AXIS2_PLACEMENT_3D ( 'NONE', #56494, #12915, #78934 ) ;
#124761=LINE ( 'NONE', #124055, #2293 ) ;
#124763=CARTESIAN_POINT ( 'NONE',  ( 69.18398860626899705, 28.73617430169835529, 5.000000000000000000 ) ) ;
#124764=VECTOR ( 'NONE', #43295, 1000.000000000000000 ) ;
#124765=VECTOR ( 'NONE', #77051, 1000.000000000000000 ) ;
#124766=EDGE_LOOP ( 'NONE', ( #8401, #56534, #58242 ) ) ;
#124767=DIRECTION ( 'NONE',  ( 1.000000000000000000, 0.000000000000000000, 0.000000000000000000 ) ) ;
#124768=DIRECTION ( 'NONE',  ( 0.6830127018922181881, 0.6830127018922202975, -0.2588190451025214056 ) ) ;
#124772=CARTESIAN_POINT ( 'NONE',  ( 11.99451991528749417, 28.92564299267946382, 4.000000000000000000 ) ) ;
#124773=FACE_OUTER_BOUND ( 'NONE', #113087, .T. ) ;
#124774=LINE ( 'NONE', #47964, #83577 ) ;
#124775=VERTEX_POINT ( 'NONE', #13651 ) ;
#124776=LINE ( 'NONE', #15971, #47337 ) ;
#124777=EDGE_LOOP ( 'NONE', ( #69049, #64228, #4432 ) ) ;
#124778=DIRECTION ( 'NONE',  ( 1.000000000000000000, 0.000000000000000000, 0.000000000000000000 ) ) ;
#124779=CARTESIAN_POINT ( 'NONE',  ( -78.18398860626899705, 28.73617430169841924, 5.000000000000000000 ) ) ;
#124782=CARTESIAN_POINT ( 'NONE',  ( 48.18398860626899705, 28.73617430169820608, 5.000000000000000000 ) ) ;
#124784=ORIENTED_EDGE ( 'NONE', *, *, #12360, .T. ) ;
#124785=PLANE ( 'NONE',  #11190 ) ;
#124786=VECTOR ( 'NONE', #69226, 1000.000000000000227 ) ;
#124788=LINE ( 'NONE', #69732, #120866 ) ;
#124789=ORIENTED_EDGE ( 'NONE', *, *, #142510, .F. ) ;
#124790=CARTESIAN_POINT ( 'NONE',  ( -4.499999999999968914, 7.087461875839175640, 4.000000000000000000 ) ) ;
#124791=VECTOR ( 'NONE', #62114, 1000.000000000000000 ) ;
#124792=CARTESIAN_POINT ( 'NONE',  ( -15.79333936457836707, 21.75929247661549937, 4.998822639870700080 ) ) ;
#124793=AXIS2_PLACEMENT_3D ( 'NONE', #96605, #74195, #140169 ) ;
#124794=ORIENTED_EDGE ( 'NONE', *, *, #132212, .T. ) ;
#124795=VECTOR ( 'NONE', #14252, 999.9999999999998863 ) ;
#124797=PLANE ( 'NONE',  #34736 ) ;
#124798=ORIENTED_EDGE ( 'NONE', *, *, #33220, .F. ) ;
#124800=ORIENTED_EDGE ( 'NONE', *, *, #83462, .F. ) ;
#124802=AXIS2_PLACEMENT_3D ( 'NONE', #19980, #20700, #43907 ) ;
#124806=DIRECTION ( 'NONE',  ( 0.7071067811865487940, 0.7071067811865463515, 0.000000000000000000 ) ) ;
#124807=ORIENTED_EDGE ( 'NONE', *, *, #22315, .T. ) ;
#124808=EDGE_CURVE ( 'NONE', #119425, #136749, #24548, .T. ) ;
#124810=DIRECTION ( 'NONE',  ( -0.000000000000000000, 0.3543493200069153248, 0.9351131265310292928 ) ) ;
#124811=CARTESIAN_POINT ( 'NONE',  ( -34.92500000000001137, -0.1586646689214904482, -3.482007288379085796 ) ) ;
#124812=CARTESIAN_POINT ( 'NONE',  ( 53.99451991528749062, 28.92564299267975869, 4.000000000000000000 ) ) ;
#124813=AXIS2_PLACEMENT_3D ( 'NONE', #60461, #6707, #50990 ) ;
#124815=DIRECTION ( 'NONE',  ( 0.7071067811865487940, 0.7071067811865463515, 0.000000000000000000 ) ) ;
#124816=PLANE ( 'NONE',  #18688 ) ;
#124817=CARTESIAN_POINT ( 'NONE',  ( 53.99451991528749062, 28.92564299267975869, 4.000000000000000000 ) ) ;
#124818=ORIENTED_EDGE ( 'NONE', *, *, #79983, .F. ) ;
#124819=EDGE_CURVE ( 'NONE', #25787, #37639, #44934, .T. ) ;
#124820=VERTEX_POINT ( 'NONE', #56523 ) ;
#124823=ORIENTED_EDGE ( 'NONE', *, *, #139487, .F. ) ;
#124824=VERTEX_POINT ( 'NONE', #70255 ) ;
#124825=ORIENTED_EDGE ( 'NONE', *, *, #122230, .F. ) ;
#124826=CYLINDRICAL_SURFACE ( 'NONE', #112724, 3.378199999999994319 ) ;
#124827=CARTESIAN_POINT ( 'NONE',  ( 34.92499999999998295, 18.00612307739178064, 4.000000000000000000 ) ) ;
#124828=EDGE_CURVE ( 'NONE', #135494, #87458, #113704, .T. ) ;
#124830=LINE ( 'NONE', #136409, #25337 ) ;
#124834=ORIENTED_EDGE ( 'NONE', *, *, #106639, .F. ) ;
#124835=FACE_OUTER_BOUND ( 'NONE', #97707, .T. ) ;
#124836=FACE_OUTER_BOUND ( 'NONE', #73483, .T. ) ;
#124837=DIRECTION ( 'NONE',  ( 0.7071067811865486830, -0.7071067811865464625, -0.000000000000000000 ) ) ;
#124839=DIRECTION ( 'NONE',  ( -0.7071067811865486830, -0.7071067811865464625, 0.000000000000000000 ) ) ;
#124840=PLANE ( 'NONE',  #44567 ) ;
#124841=CARTESIAN_POINT ( 'NONE',  ( -57.18398860626899705, 28.73617430169827358, 5.000000000000000000 ) ) ;
#124843=PLANE ( 'NONE',  #106975 ) ;
#124844=LINE ( 'NONE', #127721, #29870 ) ;
#124848=ORIENTED_EDGE ( 'NONE', *, *, #11465, .T. ) ;
#124850=LINE ( 'NONE', #72671, #4586 ) ;
#124851=ADVANCED_FACE ( 'NONE', ( #102845 ), #47776, .F. ) ;
#124852=DIRECTION ( 'NONE',  ( 0.6830127018922181881, 0.6830127018922202975, -0.2588190451025214056 ) ) ;
#124853=VERTEX_POINT ( 'NONE', #1345 ) ;
#124854=FACE_OUTER_BOUND ( 'NONE', #28609, .T. ) ;
#124855=CARTESIAN_POINT ( 'NONE',  ( 4.499999999999983125, 19.08746187583904330, 4.000000000000000000 ) ) ;
#124857=EDGE_CURVE ( 'NONE', #3513, #8091, #133333, .T. ) ;
#124859=ORIENTED_EDGE ( 'NONE', *, *, #39565, .T. ) ;
#124862=ORIENTED_EDGE ( 'NONE', *, *, #103834, .F. ) ;
#124863=CARTESIAN_POINT ( 'NONE',  ( 23.99999999999985079, 17.58746187583907172, 4.000000000000000000 ) ) ;
#124866=CIRCLE ( 'NONE', #103926, 5.968999999999998529 ) ;
#124867=ADVANCED_FACE ( 'NONE', ( #2791 ), #80391, .T. ) ;
#124868=CARTESIAN_POINT ( 'NONE',  ( 12.32816939922345334, -0.7407075233842701500, 4.000000000000000000 ) ) ;
#124870=DIRECTION ( 'NONE',  ( 0.7071067811865487940, 0.7071067811865463515, -0.000000000000000000 ) ) ;
#124871=VERTEX_POINT ( 'NONE', #23085 ) ;
#124872=EDGE_CURVE ( 'NONE', #13885, #99232, #67367, .T. ) ;
#124873=ORIENTED_EDGE ( 'NONE', *, *, #120766, .F. ) ;
#124876=CARTESIAN_POINT ( 'NONE',  ( -30.98911971346031180, -22.02621442084248216, 4.990779571109225543 ) ) ;
#124878=DIRECTION ( 'NONE',  ( 0.6830127018922181881, 0.6830127018922202975, -0.2588190451025214056 ) ) ;
#124879=PLANE ( 'NONE',  #69417 ) ;
#124880=AXIS2_PLACEMENT_3D ( 'NONE', #100044, #69578, #89854 ) ;
#124883=CARTESIAN_POINT ( 'NONE',  ( 39.29974487139159578, -27.71228299555233576, 4.000000000000000000 ) ) ;
#124885=EDGE_LOOP ( 'NONE', ( #79587, #137920, #121350, #69395 ) ) ;
#124886=EDGE_LOOP ( 'NONE', ( #94412, #12390, #117027 ) ) ;
#124887=VECTOR ( 'NONE', #99474, 1000.000000000000000 ) ;
#124888=VECTOR ( 'NONE', #54730, 1000.000000000000000 ) ;
#124889=CARTESIAN_POINT ( 'NONE',  ( 34.92499999999998295, -22.22500000000000142, 4.500000000000000888 ) ) ;
#124890=ADVANCED_FACE ( 'NONE', ( #2044 ), #17245, .T. ) ;
#124891=VERTEX_POINT ( 'NONE', #7036 ) ;
#124893=LINE ( 'NONE', #112593, #28021 ) ;
#124894=EDGE_LOOP ( 'NONE', ( #52252, #69234, #125820, #133457 ) ) ;
#124895=CARTESIAN_POINT ( 'NONE',  ( -32.67183060077624646, -0.7407075233842805861, 4.000000000000000000 ) ) ;
#124896=VECTOR ( 'NONE', #35769, 1000.000000000000114 ) ;
#124897=AXIS2_PLACEMENT_3D ( 'NONE', #12485, #15319, #13183 ) ;
#124899=FACE_BOUND ( 'NONE', #62630, .T. ) ;
#124900=CARTESIAN_POINT ( 'NONE',  ( -29.99451991528749417, 28.92564299267958816, 4.000000000000000000 ) ) ;
#124901=DIRECTION ( 'NONE',  ( -0.000000000000000000, 0.000000000000000000, 1.000000000000000000 ) ) ;
#124902=DIRECTION ( 'NONE',  ( 0.6830127018922180770, -0.6830127018922204085, -0.2588190451025213501 ) ) ;
#124905=EDGE_LOOP ( 'NONE', ( #139957, #132566, #86929, #132064 ) ) ;
#124906=VECTOR ( 'NONE', #3064, 999.9999999999998863 ) ;
#124907=AXIS2_PLACEMENT_3D ( 'NONE', #124063, #89985, #34927 ) ;
#124908=DIRECTION ( 'NONE',  ( -0.000000000000000000, -0.3543493200069152693, 0.9351131265310292928 ) ) ;
#124910=EDGE_CURVE ( 'NONE', #16142, #51777, #18644, .T. ) ;
#124911=EDGE_CURVE ( 'NONE', #31681, #64729, #103516, .T. ) ;
#124912=EDGE_LOOP ( 'NONE', ( #14924, #11287, #65891, #121242 ) ) ;
#124916=VERTEX_POINT ( 'NONE', #6311 ) ;
#124917=DIRECTION ( 'NONE',  ( -0.7071067811865487940, 0.7071067811865463515, 0.000000000000000000 ) ) ;
#124918=VECTOR ( 'NONE', #71349, 1000.000000000000000 ) ;
#124919=ADVANCED_FACE ( 'NONE', ( #73088 ), #71644, .F. ) ;
#124920=DIRECTION ( 'NONE',  ( 0.7071067811865486830, -0.7071067811865464625, -0.000000000000000000 ) ) ;
#124921=CARTESIAN_POINT ( 'NONE',  ( 5.510786437626906675, -27.52281430457051314, 5.000000000000000000 ) ) ;
#124922=PLANE ( 'NONE',  #104867 ) ;
#124924=ORIENTED_EDGE ( 'NONE', *, *, #52200, .F. ) ;
#124925=ORIENTED_EDGE ( 'NONE', *, *, #96809, .F. ) ;
#124926=CARTESIAN_POINT ( 'NONE',  ( 14.24890464969599968, -0.3792994071806725653, 4.162343009174986896 ) ) ;
#124927=DIRECTION ( 'NONE',  ( 0.7071067811865487940, 0.7071067811865463515, -0.000000000000000000 ) ) ;
#124928=ORIENTED_EDGE ( 'NONE', *, *, #61724, .F. ) ;
#124929=ORIENTED_EDGE ( 'NONE', *, *, #89872, .F. ) ;
#124931=CARTESIAN_POINT ( 'NONE',  ( -4.499999999999962697, -7.912538124160678699, 4.000000000000000000 ) ) ;
#124932=ORIENTED_EDGE ( 'NONE', *, *, #140245, .F. ) ;
#124933=DIRECTION ( 'NONE',  ( -0.000000000000000000, 0.000000000000000000, 1.000000000000000000 ) ) ;
#124936=CARTESIAN_POINT ( 'NONE',  ( 8.671830600776406328, -0.7407075233842701500, 4.000000000000000000 ) ) ;
#124937=VERTEX_POINT ( 'NONE', #128855 ) ;
#124938=LINE ( 'NONE', #111946, #45781 ) ;
#124939=CARTESIAN_POINT ( 'NONE',  ( -34.92500000000001137, 21.72500000000000142, 5.000000000000000000 ) ) ;
#124940=EDGE_CURVE ( 'NONE', #52654, #28957, #49902, .T. ) ;
#124941=CARTESIAN_POINT ( 'NONE',  ( -10.82816939922345156, 6.759292476615645917, 4.000000000000000000 ) ) ;
#124942=CARTESIAN_POINT ( 'NONE',  ( 57.18398860626899705, 28.73617430169827358, 5.000000000000000000 ) ) ;
#124943=ORIENTED_EDGE ( 'NONE', *, *, #16223, .F. ) ;
#124944=EDGE_LOOP ( 'NONE', ( #71384, #109190, #66871, #134299 ) ) ;
#124945=DIRECTION ( 'NONE',  ( -0.000000000000000000, 1.000000000000000000, -0.000000000000000000 ) ) ;
#124946=CARTESIAN_POINT ( 'NONE',  ( -17.39513766812467921, 21.75929247661549937, 21.32995629748190325 ) ) ;
#124948=ORIENTED_EDGE ( 'NONE', *, *, #85662, .F. ) ;
#124949=LINE ( 'NONE', #118145, #78313 ) ;
#124951=DIRECTION ( 'NONE',  ( -0.6830127018922181881, 0.6830127018922202975, -0.2588190451025214056 ) ) ;
#124952=VECTOR ( 'NONE', #99550, 999.9999999999998863 ) ;
#124953=VERTEX_POINT ( 'NONE', #115090 ) ;
#124954=VECTOR ( 'NONE', #30642, 1000.000000000000000 ) ;
#124955=AXIS2_PLACEMENT_3D ( 'NONE', #65455, #110324, #87173 ) ;
#124956=VECTOR ( 'NONE', #7887, 999.9999999999998863 ) ;
#124958=PLANE ( 'NONE',  #118764 ) ;
#124959=( BOUNDED_CURVE ( )  B_SPLINE_CURVE ( 3, ( #52584, #119258, #17793, #28719 ),
 .UNSPECIFIED., .F., .T. ) 
 B_SPLINE_CURVE_WITH_KNOTS ( ( 4, 4 ),
 ( 4.350170835173033268, 4.500739107949210727 ),
 .UNSPECIFIED. ) 
 CURVE ( )  GEOMETRIC_REPRESENTATION_ITEM ( )  RATIONAL_B_SPLINE_CURVE ( ( 1.000000000000000000, 0.9981116584018959736, 0.9981116584018959736, 1.000000000000000000 ) ) 
 REPRESENTATION_ITEM ( '' )  );
#124961=AXIS2_PLACEMENT_3D ( 'NONE', #45965, #48094, #102484 ) ;
#124962=EDGE_CURVE ( 'NONE', #43532, #113219, #128171, .T. ) ;
#124964=CARTESIAN_POINT ( 'NONE',  ( -11.70025512860841133, -27.71228299555198049, 4.000000000000000000 ) ) ;
#124965=ADVANCED_FACE ( 'NONE', ( #60060 ), #16510, .T. ) ;
#124966=VERTEX_POINT ( 'NONE', #81833 ) ;
#124967=ORIENTED_EDGE ( 'NONE', *, *, #73669, .F. ) ;
#124969=VECTOR ( 'NONE', #16781, 1000.000000000000227 ) ;
#124970=DIRECTION ( 'NONE',  ( -0.000000000000000000, 0.3543493200069153248, 0.9351131265310292928 ) ) ;
#124971=ADVANCED_FACE ( 'NONE', ( #94080 ), #82512, .F. ) ;
#124974=CARTESIAN_POINT ( 'NONE',  ( 54.29974487139159578, -27.71228299555243879, 4.000000000000000000 ) ) ;
#124975=VECTOR ( 'NONE', #24924, 1000.000000000000114 ) ;
#124976=CARTESIAN_POINT ( 'NONE',  ( 34.92499999999998295, 22.22500000000000142, 4.000000000000000000 ) ) ;
#124977=PLANE ( 'NONE',  #27480 ) ;
#124978=CARTESIAN_POINT ( 'NONE',  ( -32.99451991528749062, 28.92564299267960948, 4.000000000000000000 ) ) ;
#124979=EDGE_LOOP ( 'NONE', ( #85958, #1440, #42019, #6727 ) ) ;
#124982=CARTESIAN_POINT ( 'NONE',  ( -3.656710001662112131, 3.759292476615685441, 13.27625715073264523 ) ) ;
#124983=VECTOR ( 'NONE', #59599, 1000.000000000000000 ) ;
#124984=VECTOR ( 'NONE', #25159, 1000.000000000000000 ) ;
#124987=DIRECTION ( 'NONE',  ( 0.7071067811865487940, -0.7071067811865463515, 0.000000000000000000 ) ) ;
#124988=EDGE_CURVE ( 'NONE', #56522, #64090, #94848, .T. ) ;
#124991=EDGE_LOOP ( 'NONE', ( #4905, #125212, #54853, #44465, #125432 ) ) ;
#124992=LINE ( 'NONE', #25672, #80744 ) ;
#124994=CARTESIAN_POINT ( 'NONE',  ( -33.18398860626899705, 28.73617430169810305, 5.000000000000000000 ) ) ;
#124996=EDGE_CURVE ( 'NONE', #37520, #130798, #60622, .T. ) ;
#124997=VECTOR ( 'NONE', #100068, 1000.000000000000227 ) ;
#124998=LINE ( 'NONE', #93090, #78549 ) ;
#124999=DIRECTION ( 'NONE',  ( 0.7071067811865487940, 0.7071067811865463515, 0.000000000000000000 ) ) ;
#125000=CARTESIAN_POINT ( 'NONE',  ( -30.18398860626900060, 28.73617430169808173, 5.000000000000000000 ) ) ;
#125001=CARTESIAN_POINT ( 'NONE',  ( -0.4892135623730947680, -27.52281430457055578, 5.000000000000000000 ) ) ;
#125002=VECTOR ( 'NONE', #91205, 1000.000000000000000 ) ;
#125003=ORIENTED_EDGE ( 'NONE', *, *, #15228, .F. ) ;
#125004=ORIENTED_EDGE ( 'NONE', *, *, #136620, .F. ) ;
#125005=LINE ( 'NONE', #114128, #94956 ) ;
#125007=EDGE_CURVE ( 'NONE', #22876, #141378, #54202, .T. ) ;
#125008=CARTESIAN_POINT ( 'NONE',  ( 33.18398860626899705, 28.73617430169810305, 5.000000000000000000 ) ) ;
#125011=LINE ( 'NONE', #39456, #15983 ) ;
#125012=ORIENTED_EDGE ( 'NONE', *, *, #123166, .T. ) ;
#125014=CARTESIAN_POINT ( 'NONE',  ( -0.7933393645784717618, 21.75929247661549581, 4.998822639870701856 ) ) ;
#125015=FACE_OUTER_BOUND ( 'NONE', #119906, .T. ) ;
#125016=LINE ( 'NONE', #114140, #98400 ) ;
#125017=ADVANCED_FACE ( 'NONE', ( #65060 ), #63641, .T. ) ;
#125019=ORIENTED_EDGE ( 'NONE', *, *, #137864, .T. ) ;
#125020=PLANE ( 'NONE',  #2733 ) ;
#125021=EDGE_CURVE ( 'NONE', #133299, #49766, #141912, .T. ) ;
#125022=DIRECTION ( 'NONE',  ( 0.6830127018922181881, 0.6830127018922202975, -0.2588190451025214056 ) ) ;
#125024=EDGE_CURVE ( 'NONE', #135734, #105207, #131730, .T. ) ;
#125025=PLANE ( 'NONE',  #66829 ) ;
#125026=EDGE_LOOP ( 'NONE', ( #110212, #123993, #78801, #35714 ) ) ;
#125027=ORIENTED_EDGE ( 'NONE', *, *, #27618, .F. ) ;
#125028=VECTOR ( 'NONE', #8123, 1000.000000000000000 ) ;
#125029=ADVANCED_FACE ( 'NONE', ( #107803 ), #86082, .F. ) ;
#125031=DIRECTION ( 'NONE',  ( 0.7071067811865487940, 0.7071067811865463515, 0.000000000000000000 ) ) ;
#125032=PLANE ( 'NONE',  #41686 ) ;
#125033=CARTESIAN_POINT ( 'NONE',  ( 60.18398860626900415, 28.73617430169829490, 5.000000000000000000 ) ) ;
#125035=ORIENTED_EDGE ( 'NONE', *, *, #64607, .F. ) ;
#125036=DIRECTION ( 'NONE',  ( 0.6830127018922180770, -0.6830127018922204085, -0.2588190451025213501 ) ) ;
#125037=PLANE ( 'NONE',  #77914 ) ;
#125038=DIRECTION ( 'NONE',  ( -0.7071067811865486830, -0.7071067811865464625, 0.000000000000000000 ) ) ;
#125039=AXIS2_PLACEMENT_3D ( 'NONE', #26575, #38182, #116444 ) ;
#125040=FACE_OUTER_BOUND ( 'NONE', #30485, .T. ) ;
#125041=VECTOR ( 'NONE', #37797, 1000.000000000000000 ) ;
#125042=ORIENTED_EDGE ( 'NONE', *, *, #124686, .T. ) ;
#125043=EDGE_LOOP ( 'NONE', ( #43931, #53791, #67302, #55152 ) ) ;
#125044=EDGE_CURVE ( 'NONE', #133299, #63176, #57642, .T. ) ;
#125046=CARTESIAN_POINT ( 'NONE',  ( 10.60343192894636033, -14.24070752338413648, 19.24067776001728447 ) ) ;
#125048=CARTESIAN_POINT ( 'NONE',  ( 20.99451991528748707, 28.92564299267952777, 4.000000000000000000 ) ) ;
#125051=PLANE ( 'NONE',  #14492 ) ;
#125052=CARTESIAN_POINT ( 'NONE',  ( 11.29289321881337926, -12.74070752338415602, 5.000000000000000000 ) ) ;
#125053=EDGE_CURVE ( 'NONE', #36381, #141411, #108493, .T. ) ;
#125054=VECTOR ( 'NONE', #24558, 1000.000000000000000 ) ;
#125055=EDGE_LOOP ( 'NONE', ( #11424, #107083, #70362, #98245 ) ) ;
#125056=ORIENTED_EDGE ( 'NONE', *, *, #129314, .T. ) ;
#125057=CARTESIAN_POINT ( 'NONE',  ( 15.51665438641034633, 22.22500000000000142, 4.500000000000000888 ) ) ;
#125058=CARTESIAN_POINT ( 'NONE',  ( 36.18398860626899705, 28.73617430169812437, 5.000000000000000000 ) ) ;
#125059=VECTOR ( 'NONE', #64891, 1000.000000000000227 ) ;
#125061=AXIS2_PLACEMENT_3D ( 'NONE', #23879, #101423, #110145 ) ;
#125062=ORIENTED_EDGE ( 'NONE', *, *, #109471, .T. ) ;
#125063=AXIS2_PLACEMENT_3D ( 'NONE', #81824, #104215, #4885 ) ;
#125064=FACE_BOUND ( 'NONE', #56390, .T. ) ;
#125065=CARTESIAN_POINT ( 'NONE',  ( 27.18398860626900060, 28.73617430169806042, 5.000000000000000000 ) ) ;
#125066=EDGE_CURVE ( 'NONE', #68801, #19998, #87507, .T. ) ;
#125067=DIRECTION ( 'NONE',  ( 0.6830127018922180770, -0.6830127018922204085, -0.2588190451025213501 ) ) ;
#125069=AXIS2_PLACEMENT_3D ( 'NONE', #119289, #76541, #52612 ) ;
#125070=LINE ( 'NONE', #68579, #138327 ) ;
#125073=VERTEX_POINT ( 'NONE', #97657 ) ;
#125074=EDGE_CURVE ( 'NONE', #113821, #6521, #32419, .T. ) ;
#125075=EDGE_LOOP ( 'NONE', ( #53636, #25901, #8499, #122536 ) ) ;
#125077=ORIENTED_EDGE ( 'NONE', *, *, #120874, .T. ) ;
#125079=AXIS2_PLACEMENT_3D ( 'NONE', #40520, #95588, #139848 ) ;
#125080=DIRECTION ( 'NONE',  ( 0.7071067811865486830, -0.7071067811865464625, -0.000000000000000000 ) ) ;
#125082=CARTESIAN_POINT ( 'NONE',  ( 6.781626882924904898, 21.74787736706805674, 4.999607392498049308 ) ) ;
#125084=DIRECTION ( 'NONE',  ( 0.3543493200069162685, -0.000000000000000000, -0.9351131265310288487 ) ) ;
#125085=ADVANCED_FACE ( 'NONE', ( #89640 ), #80228, .F. ) ;
#125086=ORIENTED_EDGE ( 'NONE', *, *, #63333, .F. ) ;
#125087=LINE ( 'NONE', #115587, #129400 ) ;
#125088=AXIS2_PLACEMENT_3D ( 'NONE', #3629, #13804, #55941 ) ;
#125089=CARTESIAN_POINT ( 'NONE',  ( 0.000000000000000000, -16.60178936734448740, 0.8616154019347507242 ) ) ;
#125090=DIRECTION ( 'NONE',  ( -0.7071067811865486830, -0.7071067811865464625, 0.000000000000000000 ) ) ;
#125091=VECTOR ( 'NONE', #113403, 1000.000000000000000 ) ;
#125092=DIRECTION ( 'NONE',  ( -0.7071067811865486830, -0.7071067811865464625, -0.000000000000000000 ) ) ;
#125093=CARTESIAN_POINT ( 'NONE',  ( -5.999999999999963585, 4.965500833774324718, -4.007596771432642591 ) ) ;
#125094=ORIENTED_EDGE ( 'NONE', *, *, #59762, .F. ) ;
#125096=CARTESIAN_POINT ( 'NONE',  ( 34.47516574401890210, -1.509482387884363064, 4.998110765256833510 ) ) ;
#125097=DIRECTION ( 'NONE',  ( -0.7071067811865486830, -0.7071067811865464625, 0.000000000000000000 ) ) ;
#125099=EDGE_LOOP ( 'NONE', ( #113874, #114899, #129218, #89256 ) ) ;
#125101=ORIENTED_EDGE ( 'NONE', *, *, #63667, .F. ) ;
#125103=VERTEX_POINT ( 'NONE', #58504 ) ;
#125106=DIRECTION ( 'NONE',  ( 1.000000000000000000, 0.000000000000000000, 0.000000000000000000 ) ) ;
#125107=ORIENTED_EDGE ( 'NONE', *, *, #88492, .T. ) ;
#125108=DIRECTION ( 'NONE',  ( 0.7071067811865487940, 0.7071067811865463515, 0.000000000000000000 ) ) ;
#125109=ORIENTED_EDGE ( 'NONE', *, *, #129371, .F. ) ;
#125110=PLANE ( 'NONE',  #141421 ) ;
#125112=CARTESIAN_POINT ( 'NONE',  ( 32.99999999999976552, -3.412538124160717778, 4.000000000000000000 ) ) ;
#125114=VERTEX_POINT ( 'NONE', #56354 ) ;
#125116=CARTESIAN_POINT ( 'NONE',  ( 34.42499999999998295, -0.02281430457060432127, 5.000000000000000000 ) ) ;
#125118=VERTEX_POINT ( 'NONE', #68633 ) ;
#125119=LINE ( 'NONE', #25808, #87513 ) ;
#125120=EDGE_LOOP ( 'NONE', ( #21183, #129568, #94426, #134376 ) ) ;
#125121=ORIENTED_EDGE ( 'NONE', *, *, #27769, .T. ) ;
#125122=EDGE_LOOP ( 'NONE', ( #53261, #100084, #122491 ) ) ;
#125123=EDGE_CURVE ( 'NONE', #135646, #54723, #13473, .T. ) ;
#125124=DIRECTION ( 'NONE',  ( -0.7071067811865486830, 0.7071067811865464625, 0.000000000000000000 ) ) ;
#125125=VECTOR ( 'NONE', #113888, 1000.000000000000000 ) ;
#125127=FACE_OUTER_BOUND ( 'NONE', #38135, .T. ) ;
#125128=EDGE_CURVE ( 'NONE', #23467, #15784, #124412, .T. ) ;
#125129=ADVANCED_FACE ( 'NONE', ( #78072 ), #78782, .F. ) ;
#125130=DIRECTION ( 'NONE',  ( -0.000000000000000000, 0.3543493200069153248, 0.9351131265310292928 ) ) ;
#125131=ORIENTED_EDGE ( 'NONE', *, *, #129699, .F. ) ;
#125138=EDGE_CURVE ( 'NONE', #19533, #39593, #119825, .T. ) ;
#125139=FACE_OUTER_BOUND ( 'NONE', #62151, .T. ) ;
#125140=DIRECTION ( 'NONE',  ( -0.000000000000000000, 0.000000000000000000, 1.000000000000000000 ) ) ;
#125141=ORIENTED_EDGE ( 'NONE', *, *, #78190, .T. ) ;
#125142=ORIENTED_EDGE ( 'NONE', *, *, #33653, .T. ) ;
#125143=EDGE_CURVE ( 'NONE', #77572, #97669, #102680, .T. ) ;
#125144=VERTEX_POINT ( 'NONE', #11324 ) ;
#125147=LINE ( 'NONE', #4025, #22172 ) ;
#125148=EDGE_CURVE ( 'NONE', #35574, #114247, #112817, .T. ) ;
#125149=DIRECTION ( 'NONE',  ( -0.7071067811865487940, 0.7071067811865463515, 0.000000000000000000 ) ) ;
#125150=AXIS2_PLACEMENT_3D ( 'NONE', #77688, #100146, #11660 ) ;
#125151=DIRECTION ( 'NONE',  ( -0.000000000000000000, 0.000000000000000000, 1.000000000000000000 ) ) ;
#125153=CARTESIAN_POINT ( 'NONE',  ( 29.99999999999979039, -21.41253812416053748, 4.000000000000000000 ) ) ;
#125154=CIRCLE ( 'NONE', #65055, 5.968999999999998529 ) ;
#125155=ADVANCED_FACE ( 'NONE', ( #57053 ), #3322, .F. ) ;
#125156=VECTOR ( 'NONE', #136627, 1000.000000000000227 ) ;
#125158=CARTESIAN_POINT ( 'NONE',  ( -36.29974487139159578, -27.71228299555231445, 4.000000000000000000 ) ) ;
#125159=CARTESIAN_POINT ( 'NONE',  ( -33.29974487139158867, -27.71228299555229313, 4.000000000000000000 ) ) ;
#125160=CARTESIAN_POINT ( 'NONE',  ( 8.700255128608413102, -27.71228299555199825, 4.000000000000000000 ) ) ;
#125161=LINE ( 'NONE', #16367, #18672 ) ;
#125163=VECTOR ( 'NONE', #108164, 999.9999999999998863 ) ;
#125165=VECTOR ( 'NONE', #36703, 1000.000000000000000 ) ;
#125166=VECTOR ( 'NONE', #112924, 999.9999999999998863 ) ;
#125168=EDGE_LOOP ( 'NONE', ( #134603, #65309, #129388, #12087 ) ) ;
#125169=VECTOR ( 'NONE', #45451, 1000.000000000000000 ) ;
#125170=EDGE_CURVE ( 'NONE', #122142, #13717, #101223, .T. ) ;
#125171=LINE ( 'NONE', #49785, #55267 ) ;
#125172=DIRECTION ( 'NONE',  ( 0.7071067811865487940, 0.7071067811865463515, 0.000000000000000000 ) ) ;
#125175=DIRECTION ( 'NONE',  ( -0.000000000000000000, -0.3543493200069152693, 0.9351131265310292928 ) ) ;
#125176=VERTEX_POINT ( 'NONE', #14216 ) ;
#125177=CARTESIAN_POINT ( 'NONE',  ( -34.82816939922327748, -5.240707523384225297, 4.000000000000000000 ) ) ;
#125178=ORIENTED_EDGE ( 'NONE', *, *, #122342, .F. ) ;
#125179=DIRECTION ( 'NONE',  ( 0.7071067811865487940, 0.7071067811865463515, 0.000000000000000000 ) ) ;
#125181=EDGE_LOOP ( 'NONE', ( #14469, #44019, #91422, #131357 ) ) ;
#125182=ADVANCED_FACE ( 'NONE', ( #35297 ), #136000, .F. ) ;
#125183=FACE_OUTER_BOUND ( 'NONE', #30667, .T. ) ;
#125185=DIRECTION ( 'NONE',  ( -0.7071067811865486830, 0.7071067811865464625, 0.000000000000000000 ) ) ;
#125186=DIRECTION ( 'NONE',  ( 0.6830127018922180770, -0.6830127018922204085, -0.2588190451025213501 ) ) ;
#125187=EDGE_LOOP ( 'NONE', ( #81575, #103920, #121465, #95177 ) ) ;
#125188=CARTESIAN_POINT ( 'NONE',  ( -23.51078643762690490, -27.52281430457038880, 5.000000000000000000 ) ) ;
#125190=DIRECTION ( 'NONE',  ( -0.3543493200069162685, -0.000000000000000000, -0.9351131265310288487 ) ) ;
#125192=LINE ( 'NONE', #133237, #23616 ) ;
#125194=DIRECTION ( 'NONE',  ( -0.6830127018922181881, 0.6830127018922202975, -0.2588190451025214056 ) ) ;
#125195=CARTESIAN_POINT ( 'NONE',  ( 26.99999999999981526, 19.55218569542896390, 5.000000000000000000 ) ) ;
#125196=EDGE_LOOP ( 'NONE', ( #42148, #143451, #2057, #5942 ) ) ;
#125197=AXIS2_PLACEMENT_3D ( 'NONE', #26979, #104538, #92954 ) ;
#125198=CARTESIAN_POINT ( 'NONE',  ( 33.48921356237309510, -27.52281430457078670, 5.000000000000000000 ) ) ;
#125199=EDGE_CURVE ( 'NONE', #103729, #120153, #90352, .T. ) ;
#125200=ORIENTED_EDGE ( 'NONE', *, *, #4694, .F. ) ;
#125201=VECTOR ( 'NONE', #67678, 1000.000000000000000 ) ;
#125203=ADVANCED_FACE ( 'NONE', ( #46918 ), #55604, .T. ) ;
#125204=VECTOR ( 'NONE', #119806, 1000.000000000000000 ) ;
#125205=CARTESIAN_POINT ( 'NONE',  ( -6.792893218813404133, 12.75929247661558996, 5.000000000000000000 ) ) ;
#125206=DIRECTION ( 'NONE',  ( -0.7071067811865487940, 0.7071067811865463515, -0.000000000000000000 ) ) ;
#125207=PLANE ( 'NONE',  #82673 ) ;
#125208=ORIENTED_EDGE ( 'NONE', *, *, #102202, .F. ) ;
#125209=LINE ( 'NONE', #68705, #21109 ) ;
#125210=EDGE_CURVE ( 'NONE', #81380, #135817, #33857, .T. ) ;
#125211=CARTESIAN_POINT ( 'NONE',  ( 12.29974487139158512, -27.71228299555214747, 4.000000000000000000 ) ) ;
#125212=ORIENTED_EDGE ( 'NONE', *, *, #114262, .F. ) ;
#125213=PLANE ( 'NONE',  #81033 ) ;
#125214=VECTOR ( 'NONE', #37268, 1000.000000000000000 ) ;
#125217=ORIENTED_EDGE ( 'NONE', *, *, #118964, .T. ) ;
#125218=DIRECTION ( 'NONE',  ( 0.000000000000000000, 0.000000000000000000, -1.000000000000000000 ) ) ;
#125219=CARTESIAN_POINT ( 'NONE',  ( -39.29974487139159578, -27.71228299555233576, 4.000000000000000000 ) ) ;
#125220=CARTESIAN_POINT ( 'NONE',  ( -30.18398860626900060, 28.73617430169808173, 5.000000000000000000 ) ) ;
#125221=ORIENTED_EDGE ( 'NONE', *, *, #94398, .F. ) ;
#125222=ORIENTED_EDGE ( 'NONE', *, *, #143042, .T. ) ;
#125227=EDGE_CURVE ( 'NONE', #116279, #2318, #111379, .T. ) ;
#125228=CARTESIAN_POINT ( 'NONE',  ( -36.48921356237310221, -27.52281430457080802, 5.000000000000000000 ) ) ;
#125230=CARTESIAN_POINT ( 'NONE',  ( -29.99999999999979039, -13.97847968911263017, -0.1324546996127494158 ) ) ;
#125231=DIRECTION ( 'NONE',  ( 0.3543493200069162685, -0.000000000000000000, -0.9351131265310288487 ) ) ;
#125232=ORIENTED_EDGE ( 'NONE', *, *, #117760, .T. ) ;
#125234=DIRECTION ( 'NONE',  ( -0.7071067811865486830, -0.7071067811865464625, 0.000000000000000000 ) ) ;
#125236=EDGE_LOOP ( 'NONE', ( #141962, #72375, #56678, #41961 ) ) ;
#125237=EDGE_CURVE ( 'NONE', #12885, #10266, #59880, .T. ) ;
#125238=CARTESIAN_POINT ( 'NONE',  ( -66.48921356237309510, -27.52281430457101763, 5.000000000000000000 ) ) ;
#125239=LINE ( 'NONE', #142199, #78019 ) ;
#125240=DIRECTION ( 'NONE',  ( 0.3543493200069162685, -0.000000000000000000, -0.9351131265310288487 ) ) ;
#125241=VECTOR ( 'NONE', #42612, 999.9999999999998863 ) ;
#125242=VERTEX_POINT ( 'NONE', #94618 ) ;
#125243=VERTEX_POINT ( 'NONE', #83053 ) ;
#125247=CARTESIAN_POINT ( 'NONE',  ( -34.82816939922328459, 0.7592924766157104211, 4.000000000000000000 ) ) ;
#125248=VECTOR ( 'NONE', #117328, 1000.000000000000000 ) ;
#125250=PLANE ( 'NONE',  #141326 ) ;
#125251=CARTESIAN_POINT ( 'NONE',  ( -27.29974487139158512, -27.71228299555225405, 4.000000000000000000 ) ) ;
#125253=ORIENTED_EDGE ( 'NONE', *, *, #53585, .F. ) ;
#125254=ORIENTED_EDGE ( 'NONE', *, *, #54701, .F. ) ;
#125256=ORIENTED_EDGE ( 'NONE', *, *, #95204, .T. ) ;
#125257=VECTOR ( 'NONE', #85529, 1000.000000000000114 ) ;
#125258=EDGE_CURVE ( 'NONE', #29217, #123150, #104054, .T. ) ;
#125259=VECTOR ( 'NONE', #75894, 1000.000000000000000 ) ;
#125261=CARTESIAN_POINT ( 'NONE',  ( -69.48921356237309510, -27.52281430457103895, 5.000000000000000000 ) ) ;
#125262=EDGE_CURVE ( 'NONE', #108299, #15522, #82355, .T. ) ;
#125263=ORIENTED_EDGE ( 'NONE', *, *, #103825, .F. ) ;
#125264=CARTESIAN_POINT ( 'NONE',  ( -35.99451991528749772, 28.92564299267963079, 4.000000000000000000 ) ) ;
#125265=CARTESIAN_POINT ( 'NONE',  ( 57.48921356237308800, -27.52281430457095368, 5.000000000000000000 ) ) ;
#125266=LINE ( 'NONE', #4858, #108673 ) ;
#125267=VECTOR ( 'NONE', #114446, 1000.000000000000000 ) ;
#125268=VECTOR ( 'NONE', #81532, 1000.000000000000000 ) ;
#125269=VECTOR ( 'NONE', #63151, 1000.000000000000227 ) ;
#125270=AXIS2_PLACEMENT_3D ( 'NONE', #70358, #25363, #126126 ) ;
#125271=FACE_OUTER_BOUND ( 'NONE', #103241, .T. ) ;
#125272=ORIENTED_EDGE ( 'NONE', *, *, #62698, .T. ) ;
#125273=VECTOR ( 'NONE', #14586, 999.9999999999998863 ) ;
#125274=DIRECTION ( 'NONE',  ( 1.000000000000000000, 0.000000000000000000, 0.000000000000000000 ) ) ;
#125275=CARTESIAN_POINT ( 'NONE',  ( -18.88837638105230710, 9.759292476615614831, 17.35367589129216981 ) ) ;
#125276=EDGE_LOOP ( 'NONE', ( #33865, #36353, #67868, #132673 ) ) ;
#125277=CARTESIAN_POINT ( 'NONE',  ( -26.99999999999981526, 15.45873954670183181, -0.03131636524287845919 ) ) ;
#125278=EDGE_LOOP ( 'NONE', ( #50241, #140705, #47945, #86514 ) ) ;
#125279=EDGE_CURVE ( 'NONE', #43782, #49277, #95345, .T. ) ;
#125280=EDGE_LOOP ( 'NONE', ( #108693, #31180, #45990, #143406 ) ) ;
#125281=DIRECTION ( 'NONE',  ( -0.000000000000000000, -0.3543493200069152693, 0.9351131265310292928 ) ) ;
#125282=VERTEX_POINT ( 'NONE', #92473 ) ;
#125283=EDGE_LOOP ( 'NONE', ( #59467, #24323, #128375, #3621 ) ) ;
#125284=AXIS2_PLACEMENT_3D ( 'NONE', #60711, #125934, #82426 ) ;
#125285=PLANE ( 'NONE',  #81202 ) ;
#125286=ORIENTED_EDGE ( 'NONE', *, *, #32704, .T. ) ;
#125287=LINE ( 'NONE', #25976, #136889 ) ;
#125288=DIRECTION ( 'NONE',  ( -0.7071067811865487940, 0.7071067811865463515, -0.000000000000000000 ) ) ;
#125290=DIRECTION ( 'NONE',  ( -0.6830127018922180770, -0.6830127018922204085, -0.2588190451025213501 ) ) ;
#125292=DIRECTION ( 'NONE',  ( 2.781805975412905274E-17, -0.3543493200069152138, 0.9351131265310292928 ) ) ;
#125293=CARTESIAN_POINT ( 'NONE',  ( 66.18398860626901126, 28.73617430169833753, 5.000000000000000000 ) ) ;
#125294=VECTOR ( 'NONE', #91652, 1000.000000000000000 ) ;
#125295=CARTESIAN_POINT ( 'NONE',  ( 19.49999999999986855, -7.533600742197656963, 5.000000000000000000 ) ) ;
#125296=DIRECTION ( 'NONE',  ( -0.000000000000000000, 0.000000000000000000, 1.000000000000000000 ) ) ;
#125297=CARTESIAN_POINT ( 'NONE',  ( -42.48921356237308800, -27.52281430457085065, 5.000000000000000000 ) ) ;
#125298=VECTOR ( 'NONE', #110426, 1000.000000000000000 ) ;
#125300=ORIENTED_EDGE ( 'NONE', *, *, #79457, .T. ) ;
#125301=AXIS2_PLACEMENT_3D ( 'NONE', #64265, #122187, #44702 ) ;
#125303=CARTESIAN_POINT ( 'NONE',  ( 36.18398860626899705, 28.73617430169812437, 5.000000000000000000 ) ) ;
#125304=EDGE_LOOP ( 'NONE', ( #59384, #139378, #142992, #21749 ) ) ;
#125306=ORIENTED_EDGE ( 'NONE', *, *, #17745, .T. ) ;
#125307=LINE ( 'NONE', #114420, #47243 ) ;
#125308=ORIENTED_EDGE ( 'NONE', *, *, #80877, .F. ) ;
#125310=DIRECTION ( 'NONE',  ( 0.6830127018922181881, 0.6830127018922202975, -0.2588190451025214056 ) ) ;
#125311=LINE ( 'NONE', #58685, #36257 ) ;
#125312=AXIS2_PLACEMENT_3D ( 'NONE', #101622, #111045, #58903 ) ;
#125314=CARTESIAN_POINT ( 'NONE',  ( 24.18398860626899705, 28.73617430169804265, 5.000000000000000000 ) ) ;
#125315=EDGE_CURVE ( 'NONE', #11548, #23039, #40292, .T. ) ;
#125316=VERTEX_POINT ( 'NONE', #93917 ) ;
#125317=EDGE_LOOP ( 'NONE', ( #56454, #54932, #80460, #46921 ) ) ;
#125318=PLANE ( 'NONE',  #14424 ) ;
#125319=EDGE_CURVE ( 'NONE', #138876, #141554, #125119, .T. ) ;
#125322=ADVANCED_FACE ( 'NONE', ( #106193 ), #105494, .F. ) ;
#125323=CARTESIAN_POINT ( 'NONE',  ( -33.32816939922329169, -3.740707523384244837, 4.000000000000000000 ) ) ;
#125325=ORIENTED_EDGE ( 'NONE', *, *, #35334, .F. ) ;
#125326=ORIENTED_EDGE ( 'NONE', *, *, #80188, .F. ) ;
#125327=EDGE_CURVE ( 'NONE', #22361, #60511, #27956, .T. ) ;
#125329=ORIENTED_EDGE ( 'NONE', *, *, #123370, .F. ) ;
#125330=DIRECTION ( 'NONE',  ( 0.3543493200069162685, -0.000000000000000000, -0.9351131265310288487 ) ) ;
#125332=CARTESIAN_POINT ( 'NONE',  ( -26.99451991528749417, 28.92564299267956685, 4.000000000000000000 ) ) ;
#125334=ADVANCED_FACE ( 'NONE', ( #14923 ), #27224, .F. ) ;
#125337=CARTESIAN_POINT ( 'NONE',  ( 34.49999999999976552, -7.912538124160671593, 4.000000000000000000 ) ) ;
#125338=LINE ( 'NONE', #70290, #126757 ) ;
#125340=LINE ( 'NONE', #49932, #125267 ) ;
#125341=FACE_OUTER_BOUND ( 'NONE', #12445, .T. ) ;
#125342=ORIENTED_EDGE ( 'NONE', *, *, #4033, .F. ) ;
#125343=VECTOR ( 'NONE', #77910, 999.9999999999998863 ) ;
#125344=CARTESIAN_POINT ( 'NONE',  ( -51.48921356237309510, -27.52281430457091460, 5.000000000000000000 ) ) ;
#125345=ORIENTED_EDGE ( 'NONE', *, *, #126376, .T. ) ;
#125346=EDGE_CURVE ( 'NONE', #16274, #5541, #5457, .T. ) ;
#125347=FACE_OUTER_BOUND ( 'NONE', #77117, .T. ) ;
#125348=ORIENTED_EDGE ( 'NONE', *, *, #10697, .F. ) ;
#125349=ORIENTED_EDGE ( 'NONE', *, *, #12296, .T. ) ;
#125350=EDGE_CURVE ( 'NONE', #80177, #21499, #116392, .T. ) ;
#125352=FACE_OUTER_BOUND ( 'NONE', #64778, .T. ) ;
#125353=VECTOR ( 'NONE', #71371, 1000.000000000000000 ) ;
#125354=ORIENTED_EDGE ( 'NONE', *, *, #73037, .F. ) ;
#125355=DIRECTION ( 'NONE',  ( -0.7071067811865486830, -0.7071067811865464625, 0.000000000000000000 ) ) ;
#125356=ORIENTED_EDGE ( 'NONE', *, *, #13336, .F. ) ;
#125357=ADVANCED_FACE ( 'NONE', ( #17085 ), #72937, .F. ) ;
#125358=CARTESIAN_POINT ( 'NONE',  ( -13.49999999999988631, 22.08746187583901843, 4.000000000000000000 ) ) ;
#125359=PLANE ( 'NONE',  #64811 ) ;
#125361=LINE ( 'NONE', #126083, #43957 ) ;
#125362=LINE ( 'NONE', #136942, #15994 ) ;
#125363=CARTESIAN_POINT ( 'NONE',  ( -17.99999999999988276, -13.39766691384885711, -10.96608748226462282 ) ) ;
#125364=PLANE ( 'NONE',  #88879 ) ;
#125365=CARTESIAN_POINT ( 'NONE',  ( 23.21837311707488638, 21.74787736706806029, 4.999607392498050196 ) ) ;
#125368=DIRECTION ( 'NONE',  ( -0.7071067811865486830, -0.7071067811865464625, -0.000000000000000000 ) ) ;
#125371=DIRECTION ( 'NONE',  ( -0.3543493200069162685, -0.000000000000000000, -0.9351131265310288487 ) ) ;
#125372=EDGE_LOOP ( 'NONE', ( #37004, #143490, #77387, #69594 ) ) ;
#125373=( BOUNDED_CURVE ( )  B_SPLINE_CURVE ( 3, ( #24425, #12110, #79581, #58548 ),
 .UNSPECIFIED., .F., .F. ) 
 B_SPLINE_CURVE_WITH_KNOTS ( ( 4, 4 ),
 ( 1.901594255663627608, 1.933014472006554740 ),
 .UNSPECIFIED. ) 
 CURVE ( )  GEOMETRIC_REPRESENTATION_ITEM ( )  RATIONAL_B_SPLINE_CURVE ( ( 1.000000000000000000, 0.9999177325257868620, 0.9999177325257868620, 1.000000000000000000 ) ) 
 REPRESENTATION_ITEM ( '' )  );
#125374=ORIENTED_EDGE ( 'NONE', *, *, #138942, .F. ) ;
#125377=VECTOR ( 'NONE', #61981, 1000.000000000000227 ) ;
#125378=ORIENTED_EDGE ( 'NONE', *, *, #76982, .T. ) ;
#125380=ADVANCED_FACE ( 'NONE', ( #117084 ), #6159, .F. ) ;
#125381=CARTESIAN_POINT ( 'NONE',  ( 11.29289321881337393, 20.25929247661551713, 5.000000000000000000 ) ) ;
#125382=CARTESIAN_POINT ( 'NONE',  ( -34.92500000000001137, 22.06445279868695408, 5.060837336147055332 ) ) ;
#125383=AXIS2_PLACEMENT_3D ( 'NONE', #30298, #52747, #141186 ) ;
#125384=AXIS2_PLACEMENT_3D ( 'NONE', #7111, #83299, #128929 ) ;
#125385=VECTOR ( 'NONE', #57811, 999.9999999999998863 ) ;
#125386=VECTOR ( 'NONE', #86739, 1000.000000000000000 ) ;
#125388=ORIENTED_EDGE ( 'NONE', *, *, #46982, .T. ) ;
#125389=CARTESIAN_POINT ( 'NONE',  ( -6.489213562373093325, -27.52281430457059841, 5.000000000000000000 ) ) ;
#125391=LINE ( 'NONE', #80470, #9381 ) ;
#125392=CARTESIAN_POINT ( 'NONE',  ( -13.49999999999990408, -14.56887692260766087, 4.000000000000000000 ) ) ;
#125394=CARTESIAN_POINT ( 'NONE',  ( 5.218373117075015166, 21.74787736706806029, 4.999607392498049308 ) ) ;
#125395=CARTESIAN_POINT ( 'NONE',  ( 9.489213562373095101, -27.52281430457062328, 5.000000000000000000 ) ) ;
#125396=VECTOR ( 'NONE', #50340, 999.9999999999998863 ) ;
#125397=CARTESIAN_POINT ( 'NONE',  ( 13.49999999999990763, -17.91344420646041158, 1.358650452708495493 ) ) ;
#125398=DIRECTION ( 'NONE',  ( 0.3543493200069162685, -0.000000000000000000, -0.9351131265310288487 ) ) ;
#125399=CARTESIAN_POINT ( 'NONE',  ( 53.99451991528749062, 28.92564299267975869, 4.000000000000000000 ) ) ;
#125401=CARTESIAN_POINT ( 'NONE',  ( -4.499999999999960920, 12.05218569542904739, 5.000000000000000000 ) ) ;
#125403=VERTEX_POINT ( 'NONE', #70775 ) ;
#125405=VERTEX_POINT ( 'NONE', #114921 ) ;
#125408=CARTESIAN_POINT ( 'NONE',  ( 34.92499999999998295, 22.22500000000000142, 4.000000000000000000 ) ) ;
#125409=CARTESIAN_POINT ( 'NONE',  ( 31.49999999999979039, -20.94781430457059912, 5.000000000000000000 ) ) ;
#125410=ORIENTED_EDGE ( 'NONE', *, *, #136456, .F. ) ;
#125411=DIRECTION ( 'NONE',  ( 0.6830127018922180770, -0.6830127018922202975, -0.2588190451025213501 ) ) ;
#125412=DIRECTION ( 'NONE',  ( -0.6830127018922180770, -0.6830127018922204085, -0.2588190451025213501 ) ) ;
#125413=VECTOR ( 'NONE', #97041, 1000.000000000000000 ) ;
#125414=VECTOR ( 'NONE', #12002, 1000.000000000000000 ) ;
#125417=ADVANCED_FACE ( 'NONE', ( #74334 ), #96050, .F. ) ;
#125420=CARTESIAN_POINT ( 'NONE',  ( 8.229957205422008926, 21.73644205237998150, 5.000000000000000888 ) ) ;
#125423=PLANE ( 'NONE',  #135765 ) ;
#125425=VERTEX_POINT ( 'NONE', #40980 ) ;
#125426=EDGE_CURVE ( 'NONE', #95280, #122630, #84499, .T. ) ;
#125427=ORIENTED_EDGE ( 'NONE', *, *, #132683, .F. ) ;
#125428=DIRECTION ( 'NONE',  ( -0.000000000000000000, -0.3543493200069152693, 0.9351131265310292928 ) ) ;
#125429=VECTOR ( 'NONE', #14173, 999.9999999999998863 ) ;
#125431=LINE ( 'NONE', #14515, #43136 ) ;
#125432=ORIENTED_EDGE ( 'NONE', *, *, #98797, .T. ) ;
#125433=ORIENTED_EDGE ( 'NONE', *, *, #142457, .T. ) ;
#125434=DIRECTION ( 'NONE',  ( 0.000000000000000000, 1.000000000000000000, 0.000000000000000000 ) ) ;
#125435=VERTEX_POINT ( 'NONE', #53259 ) ;
#125436=ORIENTED_EDGE ( 'NONE', *, *, #81017, .F. ) ;
#125437=AXIS2_PLACEMENT_3D ( 'NONE', #105589, #117873, #60735 ) ;
#125438=AXIS2_PLACEMENT_3D ( 'NONE', #60298, #39980, #15299 ) ;
#125439=EDGE_CURVE ( 'NONE', #39694, #4634, #140289, .T. ) ;
#125440=DIRECTION ( 'NONE',  ( -0.000000000000000000, -0.3543493200069152693, 0.9351131265310292928 ) ) ;
#125441=DIRECTION ( 'NONE',  ( 0.6830127018922180770, -0.6830127018922204085, -0.2588190451025213501 ) ) ;
#125442=ADVANCED_FACE ( 'NONE', ( #10465 ), #129393, .F. ) ;
#125444=DIRECTION ( 'NONE',  ( -0.3543493200069163240, 0.000000000000000000, -0.9351131265310288487 ) ) ;
#125445=CARTESIAN_POINT ( 'NONE',  ( -23.22995720542189346, 21.73644205237998150, 5.000000000000000888 ) ) ;
#125447=DIRECTION ( 'NONE',  ( -0.000000000000000000, -0.3543493200069152693, 0.9351131265310292928 ) ) ;
#125448=DIRECTION ( 'NONE',  ( 0.6830127018922181881, 0.6830127018922202975, -0.2588190451025214056 ) ) ;
#125449=CARTESIAN_POINT ( 'NONE',  ( -34.92500000000001137, 14.19452376399130600, 8.043047640789321662 ) ) ;
#125450=FACE_BOUND ( 'NONE', #119853, .T. ) ;
#125452=FACE_OUTER_BOUND ( 'NONE', #80371, .T. ) ;
#125453=DIRECTION ( 'NONE',  ( -0.3543493200069162685, -0.000000000000000000, -0.9351131265310288487 ) ) ;
#125454=CARTESIAN_POINT ( 'NONE',  ( 26.99999999999980105, 8.587461875839165870, 4.000000000000000000 ) ) ;
#125455=EDGE_CURVE ( 'NONE', #87892, #34731, #73609, .T. ) ;
#125456=EDGE_LOOP ( 'NONE', ( #119983, #58493, #118817, #68965 ) ) ;
#125457=CARTESIAN_POINT ( 'NONE',  ( -27.88837638105224315, 9.759292476615614831, 17.35367589129219112 ) ) ;
#125458=ORIENTED_EDGE ( 'NONE', *, *, #38651, .F. ) ;
#125459=ORIENTED_EDGE ( 'NONE', *, *, #95599, .F. ) ;
#125460=AXIS2_PLACEMENT_3D ( 'NONE', #91331, #59426, #15145 ) ;
#125463=VERTEX_POINT ( 'NONE', #119923 ) ;
#125464=CARTESIAN_POINT ( 'NONE',  ( 11.99999999999992006, 7.007997736742456851, -8.085015511992084569 ) ) ;
#125465=FACE_OUTER_BOUND ( 'NONE', #74244, .T. ) ;
#125466=LINE ( 'NONE', #67537, #135314 ) ;
#125467=VERTEX_POINT ( 'NONE', #20629 ) ;
#125470=VECTOR ( 'NONE', #46549, 1000.000000000000227 ) ;
#125472=DIRECTION ( 'NONE',  ( -0.7071067811865486830, -0.7071067811865464625, 0.000000000000000000 ) ) ;
#125474=AXIS2_PLACEMENT_3D ( 'NONE', #12558, #33639, #100306 ) ;
#125476=PLANE ( 'NONE',  #62520 ) ;
#125478=DIRECTION ( 'NONE',  ( -0.7071067811865487940, 0.7071067811865463515, -0.000000000000000000 ) ) ;
#125480=ORIENTED_EDGE ( 'NONE', *, *, #118996, .T. ) ;
#125481=VECTOR ( 'NONE', #98972, 1000.000000000000000 ) ;
#125482=ORIENTED_EDGE ( 'NONE', *, *, #421, .T. ) ;
#125483=VECTOR ( 'NONE', #136049, 999.9999999999998863 ) ;
#125484=ORIENTED_EDGE ( 'NONE', *, *, #81284, .F. ) ;
#125486=ORIENTED_EDGE ( 'NONE', *, *, #115627, .F. ) ;
#125489=DIRECTION ( 'NONE',  ( -0.3543493200069163240, -0.000000000000000000, 0.9351131265310288487 ) ) ;
#125490=EDGE_LOOP ( 'NONE', ( #85171, #115369, #39284 ) ) ;
#125491=FACE_OUTER_BOUND ( 'NONE', #57810, .T. ) ;
#125492=ORIENTED_EDGE ( 'NONE', *, *, #138788, .T. ) ;
#125493=CARTESIAN_POINT ( 'NONE',  ( -15.71230993966017309, -21.73547319004781642, 4.999917730833664642 ) ) ;
#125494=CARTESIAN_POINT ( 'NONE',  ( 0.000000000000000000, 0.000000000000000000, 5.000000000000000000 ) ) ;
#125495=ADVANCED_FACE ( 'NONE', ( #107645 ), #52555, .F. ) ;
#125499=CARTESIAN_POINT ( 'NONE',  ( 25.49999999999982236, 6.431123077392117082, 4.000000000000000000 ) ) ;
#125500=EDGE_CURVE ( 'NONE', #128811, #120024, #54724, .T. ) ;
#125501=PLANE ( 'NONE',  #83708 ) ;
#125504=ORIENTED_EDGE ( 'NONE', *, *, #73652, .T. ) ;
#125505=PRESENTATION_STYLE_ASSIGNMENT (( #14591 ) ) ;
#125508=DIRECTION ( 'NONE',  ( 0.7071067811865487940, 0.7071067811865463515, 0.000000000000000000 ) ) ;
#125509=DIRECTION ( 'NONE',  ( -0.3543493200069162685, -0.000000000000000000, -0.9351131265310288487 ) ) ;
#125510=CARTESIAN_POINT ( 'NONE',  ( 18.70710678118641468, -15.74070752338412049, 5.000000000000000000 ) ) ;
#125511=EDGE_CURVE ( 'NONE', #87888, #32541, #142444, .T. ) ;
#125512=EDGE_CURVE ( 'NONE', #114222, #99443, #32243, .T. ) ;
#125513=LINE ( 'NONE', #5825, #84247 ) ;
#125514=ORIENTED_EDGE ( 'NONE', *, *, #25805, .F. ) ;
#125515=VECTOR ( 'NONE', #7581, 1000.000000000000000 ) ;
#125516=CARTESIAN_POINT ( 'NONE',  ( 12.29974487139158512, -27.71228299555214747, 4.000000000000000000 ) ) ;
#125517=VECTOR ( 'NONE', #32734, 1000.000000000000000 ) ;
#125518=VECTOR ( 'NONE', #20257, 1000.000000000000000 ) ;
#125519=LINE ( 'NONE', #15275, #88132 ) ;
#125520=LINE ( 'NONE', #105862, #11784 ) ;
#125521=ORIENTED_EDGE ( 'NONE', *, *, #87812, .T. ) ;
#125522=DIRECTION ( 'NONE',  ( -0.7071067811865486830, 0.7071067811865464625, 0.000000000000000000 ) ) ;
#125523=VECTOR ( 'NONE', #70521, 999.9999999999998863 ) ;
#125524=DIRECTION ( 'NONE',  ( -0.000000000000000000, 0.3543493200069153248, 0.9351131265310292928 ) ) ;
#125527=CARTESIAN_POINT ( 'NONE',  ( -27.18398860626900060, 28.73617430169806042, 5.000000000000000000 ) ) ;
#125529=ADVANCED_FACE ( 'NONE', ( #65630 ), #117777, .F. ) ;
#125530=EDGE_LOOP ( 'NONE', ( #129203, #27768, #28014, #40597 ) ) ;
#125531=LINE ( 'NONE', #15286, #42453 ) ;
#125532=DIRECTION ( 'NONE',  ( -0.000000000000000000, 0.000000000000000000, 1.000000000000000000 ) ) ;
#125533=VECTOR ( 'NONE', #35633, 1000.000000000000000 ) ;
#125534=EDGE_LOOP ( 'NONE', ( #94798, #114166, #99540, #116379 ) ) ;
#125536=EDGE_CURVE ( 'NONE', #62317, #85316, #7607, .T. ) ;
#125537=FACE_OUTER_BOUND ( 'NONE', #27807, .T. ) ;
#125538=PLANE ( 'NONE',  #62288 ) ;
#125539=( BOUNDED_CURVE ( )  B_SPLINE_CURVE ( 3, ( #128824, #70909, #61477, #116528 ),
 .UNSPECIFIED., .F., .T. ) 
 B_SPLINE_CURVE_WITH_KNOTS ( ( 4, 4 ),
 ( 2.779374508378133601, 4.199602562396796301 ),
 .UNSPECIFIED. ) 
 CURVE ( )  GEOMETRIC_REPRESENTATION_ITEM ( )  RATIONAL_B_SPLINE_CURVE ( ( 1.000000000000000000, 0.8388583629366717087, 0.8388583629366717087, 1.000000000000000000 ) ) 
 REPRESENTATION_ITEM ( '' )  );
#125541=DIRECTION ( 'NONE',  ( 0.6830127018922180770, -0.6830127018922204085, -0.2588190451025213501 ) ) ;
#125543=LINE ( 'NONE', #72627, #9599 ) ;
#125544=VECTOR ( 'NONE', #45394, 1000.000000000000000 ) ;
#125545=PLANE ( 'NONE',  #40151 ) ;
#125546=EDGE_CURVE ( 'NONE', #81589, #33976, #58333, .T. ) ;
#125547=CARTESIAN_POINT ( 'NONE',  ( -0.3281693992235289459, -3.740707523384244837, 4.000000000000000000 ) ) ;
#125548=AXIS2_PLACEMENT_3D ( 'NONE', #112348, #13004, #90598 ) ;
#125549=CARTESIAN_POINT ( 'NONE',  ( -4.499999999999970690, 22.01701374228155217, 2.453858888625641832 ) ) ;
#125550=CARTESIAN_POINT ( 'NONE',  ( 26.99451991528749417, 28.92564299267956685, 4.000000000000000000 ) ) ;
#125551=CARTESIAN_POINT ( 'NONE',  ( 7.499999999999951150, 3.653845994658396545, -4.504631822206387248 ) ) ;
#125552=ORIENTED_EDGE ( 'NONE', *, *, #33403, .T. ) ;
#125553=ORIENTED_EDGE ( 'NONE', *, *, #5562, .T. ) ;
#125554=VERTEX_POINT ( 'NONE', #90177 ) ;
#125556=ORIENTED_EDGE ( 'NONE', *, *, #100344, .T. ) ;
#125557=EDGE_LOOP ( 'NONE', ( #81167, #86677, #72573, #101226 ) ) ;
#125558=ORIENTED_EDGE ( 'NONE', *, *, #21298, .T. ) ;
#125559=ADVANCED_FACE ( 'NONE', ( #112653 ), #111201, .T. ) ;
#125560=VECTOR ( 'NONE', #82726, 1000.000000000000000 ) ;
#125566=CARTESIAN_POINT ( 'NONE',  ( -26.39513766812463658, 21.75929247661549226, 21.32995629748192457 ) ) ;
#125569=DIRECTION ( 'NONE',  ( 0.7071067811865487940, -0.7071067811865463515, 0.000000000000000000 ) ) ;
#125570=PLANE ( 'NONE',  #130255 ) ;
#125571=ADVANCED_FACE ( 'NONE', ( #32993 ), #2433, .F. ) ;
#125572=CARTESIAN_POINT ( 'NONE',  ( 0.000000000000000000, 0.000000000000000000, 5.000000000000000000 ) ) ;
#125573=AXIS2_PLACEMENT_3D ( 'NONE', #48721, #92923, #18182 ) ;
#125575=DIRECTION ( 'NONE',  ( 0.7071067811865487940, -0.7071067811865463515, 0.000000000000000000 ) ) ;
#125577=LINE ( 'NONE', #124128, #100106 ) ;
#125582=CARTESIAN_POINT ( 'NONE',  ( -33.29974487139158867, -27.71228299555229313, 4.000000000000000000 ) ) ;
#125583=VERTEX_POINT ( 'NONE', #78603 ) ;
#125584=ORIENTED_EDGE ( 'NONE', *, *, #11504, .T. ) ;
#125587=VERTEX_POINT ( 'NONE', #22747 ) ;
#125588=CARTESIAN_POINT ( 'NONE',  ( -0.1839886062690032631, 28.73617430169787568, 5.000000000000000000 ) ) ;
#125589=DIRECTION ( 'NONE',  ( -0.7071067811865487940, 0.7071067811865463515, 0.000000000000000000 ) ) ;
#125590=ORIENTED_EDGE ( 'NONE', *, *, #116340, .F. ) ;
#125591=VECTOR ( 'NONE', #115856, 1000.000000000000000 ) ;
#125592=VECTOR ( 'NONE', #74342, 1000.000000000000000 ) ;
#125593=VECTOR ( 'NONE', #139885, 999.9999999999998863 ) ;
#125594=FACE_OUTER_BOUND ( 'NONE', #90150, .T. ) ;
#125595=CARTESIAN_POINT ( 'NONE',  ( -18.48921356237309510, -27.52281430457068367, 5.000000000000000000 ) ) ;
#125596=DIRECTION ( 'NONE',  ( -0.000000000000000000, 0.000000000000000000, 1.000000000000000000 ) ) ;
#125599=ORIENTED_EDGE ( 'NONE', *, *, #142025, .F. ) ;
#125601=LINE ( 'NONE', #137183, #126632 ) ;
#125602=EDGE_LOOP ( 'NONE', ( #106799, #76925, #28056, #43866 ) ) ;
#125604=VECTOR ( 'NONE', #88661, 1000.000000000000227 ) ;
#125605=CARTESIAN_POINT ( 'NONE',  ( -12.29974487139158512, -27.71228299555214747, 4.000000000000000000 ) ) ;
#125606=DIRECTION ( 'NONE',  ( -0.7071067811865487940, 0.7071067811865463515, -0.000000000000000000 ) ) ;
#125607=DIRECTION ( 'NONE',  ( -0.7071067811865486830, -0.7071067811865464625, -0.000000000000000000 ) ) ;
#125609=ADVANCED_FACE ( 'NONE', ( #68474 ), #88051, .T. ) ;
#125610=ORIENTED_EDGE ( 'NONE', *, *, #52701, .F. ) ;
#125611=FACE_OUTER_BOUND ( 'NONE', #132621, .T. ) ;
#125612=DIRECTION ( 'NONE',  ( -0.000000000000000000, 0.000000000000000000, 1.000000000000000000 ) ) ;
#125613=DIRECTION ( 'NONE',  ( 0.6830127018922181881, 0.6830127018922202975, -0.2588190451025214056 ) ) ;
#125614=CARTESIAN_POINT ( 'NONE',  ( -11.99999999999991651, -11.35517001088073563, -1.126524801160135869 ) ) ;
#125617=CARTESIAN_POINT ( 'NONE',  ( -8.510786437626906675, -27.52281430457049183, 5.000000000000000000 ) ) ;
#125618=ORIENTED_EDGE ( 'NONE', *, *, #100434, .T. ) ;
#125619=ORIENTED_EDGE ( 'NONE', *, *, #46354, .F. ) ;
#125621=ORIENTED_EDGE ( 'NONE', *, *, #99812, .F. ) ;
#125622=VECTOR ( 'NONE', #103000, 1000.000000000000000 ) ;
#125623=CARTESIAN_POINT ( 'NONE',  ( 30.48921356237309510, -27.52281430457076894, 5.000000000000000000 ) ) ;
#125625=ADVANCED_FACE ( 'NONE', ( #110485 ), #122815, .F. ) ;
#125626=ORIENTED_EDGE ( 'NONE', *, *, #55880, .F. ) ;
#125627=AXIS2_PLACEMENT_3D ( 'NONE', #74517, #62207, #19391 ) ;
#125628=DIRECTION ( 'NONE',  ( 1.000000000000000000, 0.000000000000000000, 0.000000000000000000 ) ) ;
#125630=DIRECTION ( 'NONE',  ( -0.000000000000000000, -0.000000000000000000, 1.000000000000000000 ) ) ;
#125632=FACE_BOUND ( 'NONE', #67162, .T. ) ;
#125635=EDGE_CURVE ( 'NONE', #10662, #61952, #77893, .T. ) ;
#125636=CARTESIAN_POINT ( 'NONE',  ( -13.31312592467349454, 1.515602562757560223, 4.636692559446319528 ) ) ;
#125637=LINE ( 'NONE', #82846, #131502 ) ;
#125638=ORIENTED_EDGE ( 'NONE', *, *, #19635, .T. ) ;
#125639=CARTESIAN_POINT ( 'NONE',  ( -24.85181644961839709, 17.25929247661554200, 8.802941693769145814 ) ) ;
#125640=VERTEX_POINT ( 'NONE', #89469 ) ;
#125641=VERTEX_POINT ( 'NONE', #67769 ) ;
#125645=EDGE_CURVE ( 'NONE', #95099, #142404, #118886, .T. ) ;
#125646=DIRECTION ( 'NONE',  ( -0.3543493200069162685, -0.000000000000000000, -0.9351131265310288487 ) ) ;
#125649=VERTEX_POINT ( 'NONE', #62393 ) ;
#125650=CARTESIAN_POINT ( 'NONE',  ( -18.48921356237309510, -27.52281430457068367, 5.000000000000000000 ) ) ;
#125651=VECTOR ( 'NONE', #102008, 999.9999999999998863 ) ;
#125652=EDGE_CURVE ( 'NONE', #22237, #65842, #103195, .T. ) ;
#125653=CARTESIAN_POINT ( 'NONE',  ( -4.773258392821638552, -11.24070752338417556, 18.24660765846982002 ) ) ;
#125654=DIRECTION ( 'NONE',  ( 0.7071067811865486830, -0.7071067811865464625, -0.000000000000000000 ) ) ;
#125656=CARTESIAN_POINT ( 'NONE',  ( 0.000000000000000000, 0.000000000000000000, 5.000000000000000000 ) ) ;
#125657=DIRECTION ( 'NONE',  ( -0.7071067811865486830, 0.7071067811865464625, 0.000000000000000000 ) ) ;
#125658=ORIENTED_EDGE ( 'NONE', *, *, #54035, .F. ) ;
#125659=AXIS2_PLACEMENT_3D ( 'NONE', #58619, #59308, #103463 ) ;
#125660=EDGE_LOOP ( 'NONE', ( #142611, #100174, #125086, #51918 ) ) ;
#125662=LINE ( 'NONE', #15413, #109104 ) ;
#125663=EDGE_LOOP ( 'NONE', ( #87007, #46963, #122203, #75965 ) ) ;
#125664=ORIENTED_EDGE ( 'NONE', *, *, #8250, .T. ) ;
#125665=ORIENTED_EDGE ( 'NONE', *, *, #30590, .T. ) ;
#125667=LINE ( 'NONE', #93023, #13685 ) ;
#125669=ORIENTED_EDGE ( 'NONE', *, *, #61866, .T. ) ;
#125670=DIRECTION ( 'NONE',  ( 0.7071067811865487940, 0.7071067811865463515, 0.000000000000000000 ) ) ;
#125672=EDGE_CURVE ( 'NONE', #80245, #65242, #7240, .T. ) ;
#125673=CARTESIAN_POINT ( 'NONE',  ( 11.29289321881338637, -0.7407075233842718154, 5.000000000000000000 ) ) ;
#125674=ORIENTED_EDGE ( 'NONE', *, *, #46108, .F. ) ;
#125675=CARTESIAN_POINT ( 'NONE',  ( 11.81601139373100651, 28.73617430169779041, 5.000000000000000000 ) ) ;
#125676=EDGE_CURVE ( 'NONE', #467, #10314, #107294, .T. ) ;
#125677=LINE ( 'NONE', #45986, #58163 ) ;
#125678=CARTESIAN_POINT ( 'NONE',  ( 24.18398860626899705, 28.73617430169804265, 5.000000000000000000 ) ) ;
#125679=VECTOR ( 'NONE', #40820, 1000.000000000000000 ) ;
#125680=DIRECTION ( 'NONE',  ( 0.7071067811865487940, 0.7071067811865463515, -0.000000000000000000 ) ) ;
#125682=CARTESIAN_POINT ( 'NONE',  ( 18.48921356237309510, -27.52281430457068367, 5.000000000000000000 ) ) ;
#125683=ORIENTED_EDGE ( 'NONE', *, *, #139592, .F. ) ;
#125684=FACE_OUTER_BOUND ( 'NONE', #132599, .T. ) ;
#125687=VECTOR ( 'NONE', #77728, 999.9999999999998863 ) ;
#125688=EDGE_CURVE ( 'NONE', #143262, #23600, #14767, .T. ) ;
#125689=CARTESIAN_POINT ( 'NONE',  ( 23.99999999999981881, -22.22500000000000142, 4.412002311789994913 ) ) ;
#125690=AXIS2_PLACEMENT_3D ( 'NONE', #127977, #38106, #7576 ) ;
#125691=ORIENTED_EDGE ( 'NONE', *, *, #62281, .F. ) ;
#125693=CARTESIAN_POINT ( 'NONE',  ( 37.22674160717810565, -11.24070752338416490, 18.24660765846991239 ) ) ;
#125694=DIRECTION ( 'NONE',  ( -0.6830127018922181881, 0.6830127018922202975, -0.2588190451025214056 ) ) ;
#125695=LINE ( 'NONE', #26375, #12005 ) ;
#125696=VECTOR ( 'NONE', #88035, 999.9999999999998863 ) ;
#125697=VECTOR ( 'NONE', #132553, 999.9999999999998863 ) ;
#125698=ORIENTED_EDGE ( 'NONE', *, *, #71252, .T. ) ;
#125701=DIRECTION ( 'NONE',  ( -0.7071067811865486830, -0.7071067811865464625, 0.000000000000000000 ) ) ;
#125703=CARTESIAN_POINT ( 'NONE',  ( -0.8883763810524081261, 9.759292476615621936, 17.35367589129213073 ) ) ;
#125704=EDGE_CURVE ( 'NONE', #13028, #34174, #124949, .T. ) ;
#125706=VERTEX_POINT ( 'NONE', #18852 ) ;
#125707=EDGE_CURVE ( 'NONE', #73197, #8350, #137276, .T. ) ;
#125708=ORIENTED_EDGE ( 'NONE', *, *, #52756, .F. ) ;
#125709=CARTESIAN_POINT ( 'NONE',  ( 36.48921356237310221, -27.52281430457080802, 5.000000000000000000 ) ) ;
#125710=CARTESIAN_POINT ( 'NONE',  ( 34.49999999999975842, -12.66682484999663139, -0.6294897503863142729 ) ) ;
#125712=FACE_OUTER_BOUND ( 'NONE', #119041, .T. ) ;
#125714=DIRECTION ( 'NONE',  ( 0.7071067811865487940, 0.7071067811865463515, -0.000000000000000000 ) ) ;
#125715=DIRECTION ( 'NONE',  ( 0.7071067811865486830, -0.7071067811865464625, -0.000000000000000000 ) ) ;
#125717=FACE_OUTER_BOUND ( 'NONE', #28153, .T. ) ;
#125718=ORIENTED_EDGE ( 'NONE', *, *, #108289, .F. ) ;
#125719=CARTESIAN_POINT ( 'NONE',  ( 0.000000000000000000, 0.000000000000000000, 5.000000000000000000 ) ) ;
#125720=LINE ( 'NONE', #50296, #109436 ) ;
#125721=EDGE_CURVE ( 'NONE', #118382, #34223, #140631, .T. ) ;
#125722=CARTESIAN_POINT ( 'NONE',  ( -2.510786437626908008, -27.52281430457053446, 5.000000000000000000 ) ) ;
#125724=AXIS2_PLACEMENT_3D ( 'NONE', #50589, #62919, #107096 ) ;
#125725=CARTESIAN_POINT ( 'NONE',  ( 42.18398860626899705, 28.73617430169816700, 5.000000000000000000 ) ) ;
#125726=ORIENTED_EDGE ( 'NONE', *, *, #93238, .T. ) ;
#125727=CARTESIAN_POINT ( 'NONE',  ( -34.92500000000001137, 5.718490437204179599, 4.759050581649334255 ) ) ;
#125728=VECTOR ( 'NONE', #50274, 1000.000000000000000 ) ;
#125729=ORIENTED_EDGE ( 'NONE', *, *, #118194, .F. ) ;
#125730=FACE_OUTER_BOUND ( 'NONE', #78304, .T. ) ;
#125731=ORIENTED_EDGE ( 'NONE', *, *, #104175, .T. ) ;
#125732=EDGE_CURVE ( 'NONE', #118358, #62370, #92307, .T. ) ;
#125734=LINE ( 'NONE', #90224, #101713 ) ;
#125735=CARTESIAN_POINT ( 'NONE',  ( -18.29974487139159223, -27.71228299555219010, 4.000000000000000000 ) ) ;
#125736=DIRECTION ( 'NONE',  ( 1.000000000000000000, 0.000000000000000000, 0.000000000000000000 ) ) ;
#125737=DIRECTION ( 'NONE',  ( -0.7071067811865486830, 0.7071067811865464625, 0.000000000000000000 ) ) ;
#125739=ORIENTED_EDGE ( 'NONE', *, *, #69354, .F. ) ;
#125740=PLANE ( 'NONE',  #11639 ) ;
#125741=FACE_OUTER_BOUND ( 'NONE', #47282, .T. ) ;
#125743=EDGE_CURVE ( 'NONE', #76170, #120928, #103888, .T. ) ;
#125744=FACE_OUTER_BOUND ( 'NONE', #67324, .T. ) ;
#125745=LINE ( 'NONE', #124298, #31826 ) ;
#125746=CIRCLE ( 'NONE', #100280, 0.5000000000000004441 ) ;
#125748=EDGE_CURVE ( 'NONE', #141489, #33114, #27064, .T. ) ;
#125749=CARTESIAN_POINT ( 'NONE',  ( 27.18398860626900060, 28.73617430169806042, 5.000000000000000000 ) ) ;
#125750=VERTEX_POINT ( 'NONE', #108689 ) ;
#125751=ORIENTED_EDGE ( 'NONE', *, *, #74222, .T. ) ;
#125753=DIRECTION ( 'NONE',  ( -0.7071067811865486830, -0.7071067811865464625, 0.000000000000000000 ) ) ;
#125754=FACE_OUTER_BOUND ( 'NONE', #83722, .T. ) ;
#125755=CARTESIAN_POINT ( 'NONE',  ( 13.09320915088844650, 2.775078171252264969, 4.657771095945244966 ) ) ;
#125757=AXIS2_PLACEMENT_3D ( 'NONE', #106813, #139506, #41567 ) ;
#125758=VERTEX_POINT ( 'NONE', #122445 ) ;
#125759=EDGE_CURVE ( 'NONE', #121677, #58909, #65257, .T. ) ;
#125760=CARTESIAN_POINT ( 'NONE',  ( -51.48921356237309510, -27.52281430457091460, 5.000000000000000000 ) ) ;
#125761=DIRECTION ( 'NONE',  ( 0.7071067811865487940, 0.7071067811865463515, 0.000000000000000000 ) ) ;
#125763=FACE_OUTER_BOUND ( 'NONE', #42596, .T. ) ;
#125764=VERTEX_POINT ( 'NONE', #23110 ) ;
#125765=EDGE_LOOP ( 'NONE', ( #50194, #112606, #77545, #57556 ) ) ;
#125766=AXIS2_PLACEMENT_3D ( 'NONE', #34562, #23677, #125124 ) ;
#125767=DIRECTION ( 'NONE',  ( -0.6830127018922180770, -0.6830127018922204085, -0.2588190451025213501 ) ) ;
#125768=CARTESIAN_POINT ( 'NONE',  ( 5.994519915287488843, 28.92564299267942118, 4.000000000000000000 ) ) ;
#125769=DIRECTION ( 'NONE',  ( -8.817971600062199903E-18, 0.3543493200069153248, 0.9351131265310292928 ) ) ;
#125771=PLANE ( 'NONE',  #81236 ) ;
#125773=ORIENTED_EDGE ( 'NONE', *, *, #124001, .T. ) ;
#125774=CARTESIAN_POINT ( 'NONE',  ( -7.499999999999951150, 0.4497235411627352741, -5.599840258123558456 ) ) ;
#125775=CARTESIAN_POINT ( 'NONE',  ( 14.99999999999989519, 15.45873954670186201, -0.03131636524297733842 ) ) ;
#125776=VECTOR ( 'NONE', #55696, 1000.000000000000114 ) ;
#125777=DIRECTION ( 'NONE',  ( -0.7071067811865486830, -0.7071067811865464625, 0.000000000000000000 ) ) ;
#125779=EDGE_LOOP ( 'NONE', ( #35577, #17013, #106147, #5778 ) ) ;
#125782=PLANE ( 'NONE',  #113550 ) ;
#125783=EDGE_CURVE ( 'NONE', #32117, #53287, #78262, .T. ) ;
#125785=CARTESIAN_POINT ( 'NONE',  ( 0.000000000000000000, 0.000000000000000000, 5.000000000000000000 ) ) ;
#125786=ORIENTED_EDGE ( 'NONE', *, *, #133674, .T. ) ;
#125788=AXIS2_PLACEMENT_3D ( 'NONE', #79013, #113015, #25295 ) ;
#125789=PLANE ( 'NONE',  #120962 ) ;
#125790=FACE_OUTER_BOUND ( 'NONE', #83344, .T. ) ;
#125791=AXIS2_PLACEMENT_3D ( 'NONE', #67546, #111743, #56692 ) ;
#125792=EDGE_LOOP ( 'NONE', ( #112940, #34075, #46453, #22531 ) ) ;
#125793=CARTESIAN_POINT ( 'NONE',  ( -21.79333936457831911, 21.75929247661549226, 4.998822639870701856 ) ) ;
#125794=ADVANCED_FACE ( 'NONE', ( #100006 ), #8653, .F. ) ;
#125795=ORIENTED_EDGE ( 'NONE', *, *, #139619, .F. ) ;
#125797=DIRECTION ( 'NONE',  ( 0.7071067811865487940, 0.7071067811865463515, 0.000000000000000000 ) ) ;
#125799=ADVANCED_FACE ( 'NONE', ( #42787 ), #133356, .F. ) ;
#125800=FACE_BOUND ( 'NONE', #47849, .T. ) ;
#125801=DIRECTION ( 'NONE',  ( 0.6830127018922181881, 0.6830127018922202975, -0.2588190451025214056 ) ) ;
#125802=CARTESIAN_POINT ( 'NONE',  ( 66.18398860626901126, 28.73617430169833753, 5.000000000000000000 ) ) ;
#125803=EDGE_CURVE ( 'NONE', #94938, #81077, #55079, .T. ) ;
#125804=CARTESIAN_POINT ( 'NONE',  ( 0.000000000000000000, 0.000000000000000000, 5.000000000000000000 ) ) ;
#125805=CARTESIAN_POINT ( 'NONE',  ( 0.000000000000000000, 0.000000000000000000, 5.000000000000000000 ) ) ;
#125806=EDGE_CURVE ( 'NONE', #11091, #110710, #76109, .T. ) ;
#125807=DIRECTION ( 'NONE',  ( 1.000000000000000000, 0.000000000000000000, 0.000000000000000000 ) ) ;
#125809=VERTEX_POINT ( 'NONE', #66669 ) ;
#125811=VERTEX_POINT ( 'NONE', #64513 ) ;
#125813=EDGE_LOOP ( 'NONE', ( #71840, #117386, #48349, #12237 ) ) ;
#125815=PLANE ( 'NONE',  #14131 ) ;
#125816=LINE ( 'NONE', #94578, #67835 ) ;
#125817=AXIS2_PLACEMENT_3D ( 'NONE', #16323, #106924, #62030 ) ;
#125818=EDGE_CURVE ( 'NONE', #125750, #123892, #21726, .T. ) ;
#125820=ORIENTED_EDGE ( 'NONE', *, *, #126688, .F. ) ;
#125822=LINE ( 'NONE', #15568, #47792 ) ;
#125825=CARTESIAN_POINT ( 'NONE',  ( 0.1839886062690032631, 28.73617430169787568, 5.000000000000000000 ) ) ;
#125826=CARTESIAN_POINT ( 'NONE',  ( -20.67183060077633527, 17.25929247661555266, 4.000000000000000000 ) ) ;
#125827=DIRECTION ( 'NONE',  ( -0.7071067811865487940, 0.7071067811865463515, 0.000000000000000000 ) ) ;
#125829=DIRECTION ( 'NONE',  ( -0.000000000000000000, 0.3543493200069153248, 0.9351131265310292928 ) ) ;
#125830=EDGE_LOOP ( 'NONE', ( #31782, #94569, #16227, #10606 ) ) ;
#125831=PLANE ( 'NONE',  #45020 ) ;
#125833=FACE_OUTER_BOUND ( 'NONE', #141664, .T. ) ;
#125834=VECTOR ( 'NONE', #60642, 999.9999999999998863 ) ;
#125835=EDGE_LOOP ( 'NONE', ( #63782, #14040, #55472, #113683 ) ) ;
#125836=ORIENTED_EDGE ( 'NONE', *, *, #93308, .T. ) ;
#125837=ORIENTED_EDGE ( 'NONE', *, *, #106808, .F. ) ;
#125839=ADVANCED_FACE ( 'NONE', ( #136905 ), #2810, .F. ) ;
#125840=ORIENTED_EDGE ( 'NONE', *, *, #57594, .F. ) ;
#125842=VECTOR ( 'NONE', #88070, 1000.000000000000000 ) ;
#125844=AXIS2_PLACEMENT_3D ( 'NONE', #82595, #15168, #103604 ) ;
#125846=VERTEX_POINT ( 'NONE', #45650 ) ;
#125847=PLANE ( 'NONE',  #47953 ) ;
#125849=ORIENTED_EDGE ( 'NONE', *, *, #99858, .T. ) ;
#125852=DIRECTION ( 'NONE',  ( -1.000000000000000000, 0.000000000000000000, 0.000000000000000000 ) ) ;
#125853=CARTESIAN_POINT ( 'NONE',  ( 20.27718569542926730, -21.72500000000000853, 5.000000000000000000 ) ) ;
#125854=ORIENTED_EDGE ( 'NONE', *, *, #36970, .F. ) ;
#125856=PLANE ( 'NONE',  #120901 ) ;
#125857=CARTESIAN_POINT ( 'NONE',  ( 28.49999999999980815, 6.431123077392117082, 4.000000000000000000 ) ) ;
#125858=EDGE_CURVE ( 'NONE', #91146, #114341, #13667, .T. ) ;
#125859=ADVANCED_FACE ( 'NONE', ( #37607 ), #81853, .F. ) ;
#125860=EDGE_LOOP ( 'NONE', ( #2683, #24028, #104364, #69855, #143401, #34691 ) ) ;
#125861=DIRECTION ( 'NONE',  ( -0.6830127018922180770, -0.6830127018922204085, -0.2588190451025213501 ) ) ;
#125862=ORIENTED_EDGE ( 'NONE', *, *, #118681, .T. ) ;
#125864=VERTEX_POINT ( 'NONE', #113726 ) ;
#125865=ORIENTED_EDGE ( 'NONE', *, *, #21440, .T. ) ;
#125867=VECTOR ( 'NONE', #5295, 1000.000000000000000 ) ;
#125868=EDGE_CURVE ( 'NONE', #125809, #141911, #12264, .T. ) ;
#125869=LINE ( 'NONE', #101955, #28862 ) ;
#125871=LINE ( 'NONE', #95356, #129357 ) ;
#125872=LINE ( 'NONE', #136009, #76628 ) ;
#125874=VERTEX_POINT ( 'NONE', #125323 ) ;
#125875=LINE ( 'NONE', #120667, #79524 ) ;
#125877=DIRECTION ( 'NONE',  ( 0.7071067811865486830, -0.7071067811865464625, -0.000000000000000000 ) ) ;
#125878=ADVANCED_FACE ( 'NONE', ( #2066 ), #123914, .F. ) ;
#125879=CARTESIAN_POINT ( 'NONE',  ( 12.29974487139158512, -27.71228299555214747, 4.000000000000000000 ) ) ;
#125880=EDGE_LOOP ( 'NONE', ( #119128, #70439, #29754, #41757, #77005 ) ) ;
#125881=VERTEX_POINT ( 'NONE', #1366 ) ;
#125882=VERTEX_POINT ( 'NONE', #81119 ) ;
#125884=CARTESIAN_POINT ( 'NONE',  ( -29.99999999999978684, 7.552185695429095347, 5.000000000000000000 ) ) ;
#125886=CARTESIAN_POINT ( 'NONE',  ( -34.42500000000001137, -21.72500000000000142, 0.4999999999999995559 ) ) ;
#125887=DIRECTION ( 'NONE',  ( -0.7071067811865487940, 0.7071067811865463515, -0.000000000000000000 ) ) ;
#125890=VECTOR ( 'NONE', #134006, 1000.000000000000000 ) ;
#125892=LINE ( 'NONE', #25844, #134016 ) ;
#125893=PLANE ( 'NONE',  #115869 ) ;
#125894=DIRECTION ( 'NONE',  ( 1.000000000000000000, -0.000000000000000000, -0.000000000000000000 ) ) ;
#125895=DIRECTION ( 'NONE',  ( -0.000000000000000000, -0.3543493200069152693, 0.9351131265310292928 ) ) ;
#125897=LINE ( 'NONE', #114959, #82383 ) ;
#125898=VERTEX_POINT ( 'NONE', #102155 ) ;
#125899=CARTESIAN_POINT ( 'NONE',  ( -2.700255128608413990, -27.71228299555204089, 4.000000000000000000 ) ) ;
#125900=CARTESIAN_POINT ( 'NONE',  ( 17.99999999999988276, 17.58746187583906462, 4.000000000000000000 ) ) ;
#125901=ORIENTED_EDGE ( 'NONE', *, *, #11879, .T. ) ;
#125902=CARTESIAN_POINT ( 'NONE',  ( -44.99451991528749772, 28.92564299267969474, 4.000000000000000000 ) ) ;
#125903=CARTESIAN_POINT ( 'NONE',  ( -18.51665438641032679, 22.22500000000000142, 4.500000000000000888 ) ) ;
#125904=ORIENTED_EDGE ( 'NONE', *, *, #118638, .F. ) ;
#125907=CARTESIAN_POINT ( 'NONE',  ( -0.4892135623730947680, -27.52281430457055578, 5.000000000000000000 ) ) ;
#125908=ORIENTED_EDGE ( 'NONE', *, *, #126023, .T. ) ;
#125909=VECTOR ( 'NONE', #95840, 1000.000000000000227 ) ;
#125911=EDGE_CURVE ( 'NONE', #51489, #91902, #70277, .T. ) ;
#125913=CARTESIAN_POINT ( 'NONE',  ( -24.79289321881328334, -2.240707523384257716, 5.000000000000000000 ) ) ;
#125914=VECTOR ( 'NONE', #90599, 1000.000000000000000 ) ;
#125915=CARTESIAN_POINT ( 'NONE',  ( -33.79289321881321229, 9.759292476615621936, 5.000000000000000000 ) ) ;
#125916=EDGE_LOOP ( 'NONE', ( #6935, #90741, #30478, #77648 ) ) ;
#125917=CARTESIAN_POINT ( 'NONE',  ( 34.92499999999998295, -18.28150956279555217, 4.759050581649326261 ) ) ;
#125918=CARTESIAN_POINT ( 'NONE',  ( -20.21837311707492546, 21.74787736706806740, 4.999607392498048419 ) ) ;
#125919=DIRECTION ( 'NONE',  ( -0.6830127018922181881, 0.6830127018922202975, -0.2588190451025214056 ) ) ;
#125922=VERTEX_POINT ( 'NONE', #24570 ) ;
#125923=VECTOR ( 'NONE', #12436, 1000.000000000000227 ) ;
#125924=DIRECTION ( 'NONE',  ( -0.7071067811865486830, -0.7071067811865464625, 0.000000000000000000 ) ) ;
#125925=ORIENTED_EDGE ( 'NONE', *, *, #5726, .T. ) ;
#125928=CARTESIAN_POINT ( 'NONE',  ( 29.99999999999979039, 7.931123077392108200, 4.000000000000000000 ) ) ;
#125929=DIRECTION ( 'NONE',  ( 0.7071067811865486830, -0.7071067811865464625, -0.000000000000000000 ) ) ;
#125930=CARTESIAN_POINT ( 'NONE',  ( 27.79289321881327268, -5.240707523384227073, 5.000000000000000000 ) ) ;
#125931=VERTEX_POINT ( 'NONE', #35497 ) ;
#125932=LINE ( 'NONE', #73011, #122951 ) ;
#125933=VECTOR ( 'NONE', #29218, 1000.000000000000227 ) ;
#125934=DIRECTION ( 'NONE',  ( 0.6830127018922180770, -0.6830127018922204085, -0.2588190451025213501 ) ) ;
#125935=AXIS2_PLACEMENT_3D ( 'NONE', #97866, #63824, #141361 ) ;
#125936=LINE ( 'NONE', #124493, #85545 ) ;
#125937=CARTESIAN_POINT ( 'NONE',  ( 14.47599861414540534, 22.03583458319438648, 4.979811245910083173 ) ) ;
#125939=ORIENTED_EDGE ( 'NONE', *, *, #69080, .F. ) ;
#125940=CARTESIAN_POINT ( 'NONE',  ( 0.000000000000000000, 0.000000000000000000, 5.000000000000000000 ) ) ;
#125943=VECTOR ( 'NONE', #89790, 1000.000000000000000 ) ;
#125944=ORIENTED_EDGE ( 'NONE', *, *, #137953, .T. ) ;
#125945=ORIENTED_EDGE ( 'NONE', *, *, #119546, .F. ) ;
#125946=ORIENTED_EDGE ( 'NONE', *, *, #123005, .F. ) ;
#125948=VECTOR ( 'NONE', #10105, 1000.000000000000000 ) ;
#125950=DIRECTION ( 'NONE',  ( 0.000000000000000000, 1.000000000000000000, 0.000000000000000000 ) ) ;
#125951=DIRECTION ( 'NONE',  ( -0.7071067811865486830, -0.7071067811865464625, -0.000000000000000000 ) ) ;
#125953=VECTOR ( 'NONE', #24428, 999.9999999999998863 ) ;
#125954=DIRECTION ( 'NONE',  ( -0.7071067811865486830, -0.7071067811865464625, -0.000000000000000000 ) ) ;
#125955=PLANE ( 'NONE',  #3761 ) ;
#125956=ORIENTED_EDGE ( 'NONE', *, *, #21759, .F. ) ;
#125958=CARTESIAN_POINT ( 'NONE',  ( 17.29289321881333308, -18.74070752338409562, 5.000000000000000000 ) ) ;
#125961=ORIENTED_EDGE ( 'NONE', *, *, #105114, .F. ) ;
#125962=LINE ( 'NONE', #37533, #95281 ) ;
#125966=CARTESIAN_POINT ( 'NONE',  ( -75.48921356237309510, -27.52281430457107803, 5.000000000000000000 ) ) ;
#125967=ORIENTED_EDGE ( 'NONE', *, *, #47265, .F. ) ;
#125968=EDGE_LOOP ( 'NONE', ( #92851, #125492, #24862, #13683 ) ) ;
#125969=EDGE_CURVE ( 'NONE', #103228, #34514, #91293, .T. ) ;
#125970=DIRECTION ( 'NONE',  ( -0.7071067811865487940, 0.7071067811865463515, -0.000000000000000000 ) ) ;
#125971=ADVANCED_FACE ( 'NONE', ( #73104 ), #49919, .F. ) ;
#125972=ADVANCED_FACE ( 'NONE', ( #41154 ), #83243, .F. ) ;
#125973=LINE ( 'NONE', #106304, #15340 ) ;
#125974=DIRECTION ( 'NONE',  ( 0.7071067811865487940, 0.7071067811865463515, 0.000000000000000000 ) ) ;
#125975=LINE ( 'NONE', #29481, #4851 ) ;
#125977=CARTESIAN_POINT ( 'NONE',  ( -14.29289321881335617, 20.25929247661551003, 5.000000000000000000 ) ) ;
#125978=EDGE_CURVE ( 'NONE', #66817, #121662, #60819, .T. ) ;
#125980=LINE ( 'NONE', #127380, #25759 ) ;
#125981=VECTOR ( 'NONE', #93028, 1000.000000000000000 ) ;
#125983=VERTEX_POINT ( 'NONE', #70956 ) ;
#125985=EDGE_CURVE ( 'NONE', #14551, #143518, #116579, .T. ) ;
#125986=ORIENTED_EDGE ( 'NONE', *, *, #72818, .T. ) ;
#125987=AXIS2_PLACEMENT_3D ( 'NONE', #16874, #29865, #74109 ) ;
#125988=LINE ( 'NONE', #128819, #96366 ) ;
#125989=EDGE_CURVE ( 'NONE', #5949, #90206, #127449, .T. ) ;
#125990=DIRECTION ( 'NONE',  ( -0.000000000000000000, 0.3543493200069153248, 0.9351131265310292928 ) ) ;
#125991=ORIENTED_EDGE ( 'NONE', *, *, #52906, .T. ) ;
#125992=DIRECTION ( 'NONE',  ( -0.000000000000000000, -0.3543493200069152138, 0.9351131265310292928 ) ) ;
#125993=CARTESIAN_POINT ( 'NONE',  ( 21.18398860626899349, 28.73617430169802134, 5.000000000000000000 ) ) ;
#125994=FACE_OUTER_BOUND ( 'NONE', #101177, .T. ) ;
#125995=DIRECTION ( 'NONE',  ( -0.7071067811865486830, -0.7071067811865464625, 0.000000000000000000 ) ) ;
#125996=ORIENTED_EDGE ( 'NONE', *, *, #108255, .T. ) ;
#125998=CARTESIAN_POINT ( 'NONE',  ( 17.99999999999987566, 10.55218569542905627, 5.000000000000000000 ) ) ;
#125999=EDGE_LOOP ( 'NONE', ( #34070, #113340, #5397, #68130 ) ) ;
#126000=DIRECTION ( 'NONE',  ( 0.7071067811865487940, 0.7071067811865463515, 0.000000000000000000 ) ) ;
#126003=DIRECTION ( 'NONE',  ( -0.7071067811865487940, 0.7071067811865463515, 0.000000000000000000 ) ) ;
#126004=ORIENTED_EDGE ( 'NONE', *, *, #116494, .T. ) ;
#126005=ORIENTED_EDGE ( 'NONE', *, *, #42022, .T. ) ;
#126007=VECTOR ( 'NONE', #72914, 1000.000000000000227 ) ;
#126008=EDGE_CURVE ( 'NONE', #9115, #89845, #17942, .T. ) ;
#126009=ORIENTED_EDGE ( 'NONE', *, *, #19930, .F. ) ;
#126012=CARTESIAN_POINT ( 'NONE',  ( 20.80599055185816582, -22.22500000000000142, 26.11855565392658463 ) ) ;
#126016=CARTESIAN_POINT ( 'NONE',  ( 18.75860074219783868, 21.72500000000000853, 5.000000000000000000 ) ) ;
#126017=VECTOR ( 'NONE', #28015, 1000.000000000000000 ) ;
#126018=CARTESIAN_POINT ( 'NONE',  ( 24.59263130292903554, 0.9595543924999635488, 5.000000000000000000 ) ) ;
#126019=ADVANCED_FACE ( 'NONE', ( #139057 ), #39761, .T. ) ;
#126020=FACE_OUTER_BOUND ( 'NONE', #77850, .T. ) ;
#126023=EDGE_CURVE ( 'NONE', #46563, #63474, #71660, .T. ) ;
#126024=ORIENTED_EDGE ( 'NONE', *, *, #75173, .F. ) ;
#126025=CARTESIAN_POINT ( 'NONE',  ( 36.48921356237310221, -27.52281430457080802, 5.000000000000000000 ) ) ;
#126026=VECTOR ( 'NONE', #110671, 1000.000000000000000 ) ;
#126027=DIRECTION ( 'NONE',  ( -0.3543493200069163240, 4.681814790819596721E-17, -0.9351131265310288487 ) ) ;
#126028=EDGE_LOOP ( 'NONE', ( #49196, #94793, #32464, #125482 ) ) ;
#126029=ADVANCED_FACE ( 'NONE', ( #73792 ), #117962, .T. ) ;
#126030=VERTEX_POINT ( 'NONE', #106373 ) ;
#126031=CARTESIAN_POINT ( 'NONE',  ( 9.183988606268997046, 28.73617430169793607, 5.000000000000000000 ) ) ;
#126032=VERTEX_POINT ( 'NONE', #50613 ) ;
#126033=EDGE_CURVE ( 'NONE', #56507, #33017, #95526, .T. ) ;
#126034=FACE_OUTER_BOUND ( 'NONE', #33607, .T. ) ;
#126037=CARTESIAN_POINT ( 'NONE',  ( -19.49999999999987921, 22.22500000000000142, 4.362957392718803007 ) ) ;
#126038=DIRECTION ( 'NONE',  ( -0.3543493200069163240, 0.000000000000000000, -0.9351131265310288487 ) ) ;
#126039=EDGE_LOOP ( 'NONE', ( #136166, #18842, #93872, #19119 ) ) ;
#126040=LINE ( 'NONE', #26709, #108962 ) ;
#126041=ORIENTED_EDGE ( 'NONE', *, *, #17977, .T. ) ;
#126042=EDGE_CURVE ( 'NONE', #9815, #88923, #84670, .T. ) ;
#126043=CARTESIAN_POINT ( 'NONE',  ( 5.999999999999950262, -16.02097659208071079, -11.96015758381210148 ) ) ;
#126044=VECTOR ( 'NONE', #138509, 1000.000000000000000 ) ;
#126045=VECTOR ( 'NONE', #5986, 1000.000000000000227 ) ;
#126047=AXIS2_PLACEMENT_3D ( 'NONE', #62950, #140470, #7801 ) ;
#126048=DIRECTION ( 'NONE',  ( 0.6830127018922181881, 0.6830127018922202975, -0.2588190451025214056 ) ) ;
#126049=ADVANCED_FACE ( 'NONE', ( #128190 ), #104247, .F. ) ;
#126051=VERTEX_POINT ( 'NONE', #82531 ) ;
#126052=VERTEX_POINT ( 'NONE', #4912 ) ;
#126053=VERTEX_POINT ( 'NONE', #49210 ) ;
#126054=CARTESIAN_POINT ( 'NONE',  ( 29.86500426248360185, 3.759292476615688550, 15.36553568819719295 ) ) ;
#126056=DIRECTION ( 'NONE',  ( 0.7071067811865487940, 0.7071067811865463515, 0.000000000000000000 ) ) ;
#126057=VERTEX_POINT ( 'NONE', #107116 ) ;
#126058=DIRECTION ( 'NONE',  ( 0.3543493200069162685, -0.000000000000000000, -0.9351131265310288487 ) ) ;
#126059=PLANE ( 'NONE',  #75877 ) ;
#126060=AXIS2_PLACEMENT_3D ( 'NONE', #70746, #128665, #104019 ) ;
#126061=DIRECTION ( 'NONE',  ( 0.7071067811865487940, 0.7071067811865463515, 0.000000000000000000 ) ) ;
#126062=LINE ( 'NONE', #25289, #18763 ) ;
#126063=DIRECTION ( 'NONE',  ( -1.000000000000000000, 0.000000000000000000, 0.000000000000000000 ) ) ;
#126064=VERTEX_POINT ( 'NONE', #93402 ) ;
#126066=PLANE ( 'NONE',  #97941 ) ;
#126067=ORIENTED_EDGE ( 'NONE', *, *, #92752, .T. ) ;
#126069=CARTESIAN_POINT ( 'NONE',  ( -6.299744871391586898, -27.71228299555210484, 4.000000000000000000 ) ) ;
#126070=VERTEX_POINT ( 'NONE', #83989 ) ;
#126071=ADVANCED_FACE ( 'NONE', ( #28867 ), #7793, .F. ) ;
#126072=ORIENTED_EDGE ( 'NONE', *, *, #81633, .T. ) ;
#126073=DIRECTION ( 'NONE',  ( 0.6830127018922180770, -0.6830127018922204085, -0.2588190451025213501 ) ) ;
#126074=PLANE ( 'NONE',  #51648 ) ;
#126075=PLANE ( 'NONE',  #122485 ) ;
#126076=VERTEX_POINT ( 'NONE', #119404 ) ;
#126077=DIRECTION ( 'NONE',  ( 0.7071067811865487940, 0.7071067811865463515, 0.000000000000000000 ) ) ;
#126079=DIRECTION ( 'NONE',  ( 0.7071067811865487940, 0.7071067811865463515, 0.000000000000000000 ) ) ;
#126080=DIRECTION ( 'NONE',  ( 0.7071067811865487940, -0.7071067811865463515, 0.000000000000000000 ) ) ;
#126083=CARTESIAN_POINT ( 'NONE',  ( -9.183988606268997046, 28.73617430169793607, 5.000000000000000000 ) ) ;
#126084=CARTESIAN_POINT ( 'NONE',  ( -36.18398860626899705, 28.73617430169812437, 5.000000000000000000 ) ) ;
#126086=CARTESIAN_POINT ( 'NONE',  ( 51.29974487139158867, -27.71228299555242103, 4.000000000000000000 ) ) ;
#126087=DIRECTION ( 'NONE',  ( -0.000000000000000000, 0.3543493200069153248, 0.9351131265310292928 ) ) ;
#126090=LINE ( 'NONE', #94141, #110680 ) ;
#126091=CARTESIAN_POINT ( 'NONE',  ( 36.18398860626899705, 28.73617430169812437, 5.000000000000000000 ) ) ;
#126092=CARTESIAN_POINT ( 'NONE',  ( 2.999999999999975131, -5.527737879153189482, -7.983877177622378696 ) ) ;
#126093=ORIENTED_EDGE ( 'NONE', *, *, #67747, .F. ) ;
#126094=AXIS2_PLACEMENT_3D ( 'NONE', #4310, #92817, #111733 ) ;
#126098=EDGE_CURVE ( 'NONE', #32288, #114480, #99821, .T. ) ;
#126100=ORIENTED_EDGE ( 'NONE', *, *, #32105, .T. ) ;
#126101=LINE ( 'NONE', #15157, #4004 ) ;
#126102=CARTESIAN_POINT ( 'NONE',  ( -5.526639036357822832, -5.240707523384232402, 16.25846745537494442 ) ) ;
#126103=CARTESIAN_POINT ( 'NONE',  ( 57.48921356237308800, -27.52281430457095368, 5.000000000000000000 ) ) ;
#126105=PLANE ( 'NONE',  #134329 ) ;
#126106=DIRECTION ( 'NONE',  ( -0.000000000000000000, 0.3543493200069153248, 0.9351131265310292928 ) ) ;
#126110=CARTESIAN_POINT ( 'NONE',  ( -14.99451991528749595, 28.92564299267948513, 4.000000000000000000 ) ) ;
#126113=DIRECTION ( 'NONE',  ( -0.7071067811865487940, 0.7071067811865463515, -0.000000000000000000 ) ) ;
#126114=PLANE ( 'NONE',  #13003 ) ;
#126117=EDGE_LOOP ( 'NONE', ( #137715, #71072, #67511, #58508 ) ) ;
#126118=ORIENTED_EDGE ( 'NONE', *, *, #55618, .F. ) ;
#126120=ORIENTED_EDGE ( 'NONE', *, *, #76467, .T. ) ;
#126121=AXIS2_PLACEMENT_3D ( 'NONE', #352, #44648, #88838 ) ;
#126124=ORIENTED_EDGE ( 'NONE', *, *, #64343, .T. ) ;
#126125=PLANE ( 'NONE',  #65342 ) ;
#126126=DIRECTION ( 'NONE',  ( 0.7071067811865487940, -0.7071067811865463515, 0.000000000000000000 ) ) ;
#126129=ORIENTED_EDGE ( 'NONE', *, *, #98319, .T. ) ;
#126130=EDGE_CURVE ( 'NONE', #72096, #50134, #30280, .T. ) ;
#126131=ORIENTED_EDGE ( 'NONE', *, *, #18722, .T. ) ;
#126132=CARTESIAN_POINT ( 'NONE',  ( -5.999999999999960032, 2.342191155542443948, -5.001666872980071510 ) ) ;
#126135=VERTEX_POINT ( 'NONE', #97676 ) ;
#126136=EDGE_LOOP ( 'NONE', ( #74951, #53748, #26143, #23108 ) ) ;
#126137=ORIENTED_EDGE ( 'NONE', *, *, #50244, .F. ) ;
#126138=CARTESIAN_POINT ( 'NONE',  ( 32.99999999999977263, 2.342191155542478587, -5.001666872980161216 ) ) ;
#126139=EDGE_CURVE ( 'NONE', #22356, #90401, #55619, .T. ) ;
#126141=ADVANCED_FACE ( 'NONE', ( #64345 ), #131752, .F. ) ;
#126142=EDGE_CURVE ( 'NONE', #74888, #35249, #9192, .T. ) ;
#126144=VECTOR ( 'NONE', #113517, 1000.000000000000000 ) ;
#126145=CARTESIAN_POINT ( 'NONE',  ( -34.92500000000001137, -4.298069433178936194, 4.500000000000000888 ) ) ;
#126146=EDGE_CURVE ( 'NONE', #142842, #20535, #118709, .T. ) ;
#126147=ORIENTED_EDGE ( 'NONE', *, *, #42513, .F. ) ;
#126148=VECTOR ( 'NONE', #28814, 1000.000000000000000 ) ;
#126149=ORIENTED_EDGE ( 'NONE', *, *, #104971, .F. ) ;
#126150=CARTESIAN_POINT ( 'NONE',  ( 36.29177708983025497, -15.74070752338412760, 19.73771281079106288 ) ) ;
#126151=ADVANCED_FACE ( 'NONE', ( #43313 ), #66498, .T. ) ;
#126152=ORIENTED_EDGE ( 'NONE', *, *, #141056, .F. ) ;
#126154=EDGE_CURVE ( 'NONE', #58779, #23719, #31714, .T. ) ;
#126155=CARTESIAN_POINT ( 'NONE',  ( 19.05000000000000071, 3.174999999999997158, 4.000000000000000000 ) ) ;
#126158=ORIENTED_EDGE ( 'NONE', *, *, #136318, .F. ) ;
#126159=LINE ( 'NONE', #50732, #1979 ) ;
#126160=DIRECTION ( 'NONE',  ( -0.6830127018922181881, 0.6830127018922202975, -0.2588190451025214056 ) ) ;
#126161=EDGE_CURVE ( 'NONE', #66092, #98260, #96926, .T. ) ;
#126162=FACE_BOUND ( 'NONE', #8012, .T. ) ;
#126163=ORIENTED_EDGE ( 'NONE', *, *, #79435, .T. ) ;
#126165=CARTESIAN_POINT ( 'NONE',  ( 30.79289321881324781, 0.7592924766157104211, 5.000000000000000000 ) ) ;
#126166=FACE_OUTER_BOUND ( 'NONE', #32563, .T. ) ;
#126168=CARTESIAN_POINT ( 'NONE',  ( -19.05000000000000071, 3.174999999999997158, 5.000000000000000000 ) ) ;
#126169=ORIENTED_EDGE ( 'NONE', *, *, #52801, .T. ) ;
#126170=ORIENTED_EDGE ( 'NONE', *, *, #133281, .F. ) ;
#126171=ADVANCED_FACE ( 'NONE', ( #141171 ), #130329, .F. ) ;
#126172=ORIENTED_EDGE ( 'NONE', *, *, #97701, .F. ) ;
#126174=ORIENTED_EDGE ( 'NONE', *, *, #112990, .T. ) ;
#126175=CARTESIAN_POINT ( 'NONE',  ( 78.48921356237309510, -27.52281430457109934, 5.000000000000000000 ) ) ;
#126176=PLANE ( 'NONE',  #94624 ) ;
#126177=LINE ( 'NONE', #79861, #105275 ) ;
#126178=VERTEX_POINT ( 'NONE', #75935 ) ;
#126181=CARTESIAN_POINT ( 'NONE',  ( 25.49999999999981526, -10.91253812416064406, 4.000000000000000000 ) ) ;
#126182=CARTESIAN_POINT ( 'NONE',  ( -9.489213562373095101, -27.52281430457062328, 5.000000000000000000 ) ) ;
#126183=CARTESIAN_POINT ( 'NONE',  ( 44.99451991528749772, 28.92564299267969474, 4.000000000000000000 ) ) ;
#126184=FACE_OUTER_BOUND ( 'NONE', #89557, .T. ) ;
#126185=VERTEX_POINT ( 'NONE', #120847 ) ;
#126186=EDGE_CURVE ( 'NONE', #105516, #142230, #120109, .T. ) ;
#126187=ORIENTED_EDGE ( 'NONE', *, *, #31470, .F. ) ;
#126188=ORIENTED_EDGE ( 'NONE', *, *, #124438, .T. ) ;
#126189=ORIENTED_EDGE ( 'NONE', *, *, #25368, .F. ) ;
#126191=VERTEX_POINT ( 'NONE', #32436 ) ;
#126193=ORIENTED_EDGE ( 'NONE', *, *, #37705, .T. ) ;
#126194=PLANE ( 'NONE',  #25848 ) ;
#126196=LINE ( 'NONE', #5085, #60196 ) ;
#126197=ORIENTED_EDGE ( 'NONE', *, *, #96192, .T. ) ;
#126201=VECTOR ( 'NONE', #1951, 1000.000000000000000 ) ;
#126202=CARTESIAN_POINT ( 'NONE',  ( 15.15612307739229436, -22.22499999999999432, 4.000000000000000000 ) ) ;
#126204=EDGE_LOOP ( 'NONE', ( #19777, #91569, #18026, #43836 ) ) ;
#126206=FACE_OUTER_BOUND ( 'NONE', #106724, .T. ) ;
#126207=AXIS2_PLACEMENT_3D ( 'NONE', #101308, #56432, #121616 ) ;
#126209=ADVANCED_FACE ( 'NONE', ( #109976 ), #10644, .F. ) ;
#126210=LINE ( 'NONE', #62395, #81303 ) ;
#126211=ORIENTED_EDGE ( 'NONE', *, *, #2826, .F. ) ;
#126212=ORIENTED_EDGE ( 'NONE', *, *, #119931, .F. ) ;
#126213=PLANE ( 'NONE',  #51843 ) ;
#126214=ORIENTED_EDGE ( 'NONE', *, *, #20715, .F. ) ;
#126215=CARTESIAN_POINT ( 'NONE',  ( -9.489213562373095101, -27.52281430457062328, 5.000000000000000000 ) ) ;
#126217=DIRECTION ( 'NONE',  ( -0.000000000000000000, 0.3543493200069153248, 0.9351131265310292928 ) ) ;
#126218=LINE ( 'NONE', #114603, #49577 ) ;
#126220=ORIENTED_EDGE ( 'NONE', *, *, #133383, .F. ) ;
#126221=CARTESIAN_POINT ( 'NONE',  ( 28.49999999999979750, -14.70932175296475108, -11.46312253303843853 ) ) ;
#126222=AXIS2_PLACEMENT_3D ( 'NONE', #66696, #132702, #46408 ) ;
#126223=EDGE_CURVE ( 'NONE', #20803, #115452, #46930, .T. ) ;
#126224=CARTESIAN_POINT ( 'NONE',  ( 30.18398860626900060, 28.73617430169808173, 5.000000000000000000 ) ) ;
#126225=CARTESIAN_POINT ( 'NONE',  ( -33.48921356237309510, -27.52281430457078670, 5.000000000000000000 ) ) ;
#126227=DIRECTION ( 'NONE',  ( 0.7071067811865487940, 0.7071067811865463515, -0.000000000000000000 ) ) ;
#126228=CARTESIAN_POINT ( 'NONE',  ( -21.48921356237309155, -27.52281430457070499, 5.000000000000000000 ) ) ;
#126229=ORIENTED_EDGE ( 'NONE', *, *, #44627, .F. ) ;
#126230=PLANE ( 'NONE',  #113459 ) ;
#126232=EDGE_CURVE ( 'NONE', #74261, #107142, #24401, .T. ) ;
#126233=EDGE_LOOP ( 'NONE', ( #130359, #104763, #141313, #25833 ) ) ;
#126234=CARTESIAN_POINT ( 'NONE',  ( 34.92499999999998295, -12.28150956279560369, 4.759050581649325373 ) ) ;
#126235=DIRECTION ( 'NONE',  ( 1.000000000000000000, 0.000000000000000000, 0.000000000000000000 ) ) ;
#126236=ORIENTED_EDGE ( 'NONE', *, *, #126130, .F. ) ;
#126237=CARTESIAN_POINT ( 'NONE',  ( 34.92499999999998295, 20.82781275693360712, 4.470553524000301593 ) ) ;
#126240=VECTOR ( 'NONE', #46820, 1000.000000000000000 ) ;
#126241=LINE ( 'NONE', #141390, #131819 ) ;
#126242=ORIENTED_EDGE ( 'NONE', *, *, #66422, .T. ) ;
#126243=AXIS2_PLACEMENT_3D ( 'NONE', #108306, #8976, #136511 ) ;
#126244=DIRECTION ( 'NONE',  ( -0.7071067811865487940, 0.7071067811865463515, 0.000000000000000000 ) ) ;
#126245=DIRECTION ( 'NONE',  ( -0.7071067811865486830, -0.7071067811865464625, -0.000000000000000000 ) ) ;
#126246=AXIS2_PLACEMENT_3D ( 'NONE', #94167, #49288, #139859 ) ;
#126247=LINE ( 'NONE', #103743, #14285 ) ;
#126248=LINE ( 'NONE', #81337, #100346 ) ;
#126249=FACE_OUTER_BOUND ( 'NONE', #1457, .T. ) ;
#126250=CARTESIAN_POINT ( 'NONE',  ( 2.671830600776458287, -12.74070752338415247, 4.000000000000000000 ) ) ;
#126251=LINE ( 'NONE', #104480, #142603 ) ;
#126252=ORIENTED_EDGE ( 'NONE', *, *, #105908, .T. ) ;
#126253=ORIENTED_EDGE ( 'NONE', *, *, #142809, .T. ) ;
#126254=EDGE_LOOP ( 'NONE', ( #84291, #119791, #108230, #103329 ) ) ;
#126256=EDGE_CURVE ( 'NONE', #143315, #139444, #57780, .T. ) ;
#126257=VERTEX_POINT ( 'NONE', #113536 ) ;
#126258=VERTEX_POINT ( 'NONE', #12794 ) ;
#126259=ORIENTED_EDGE ( 'NONE', *, *, #113036, .F. ) ;
#126260=FACE_OUTER_BOUND ( 'NONE', #190, .T. ) ;
#126261=CARTESIAN_POINT ( 'NONE',  ( -5.510786437626906675, -27.52281430457051314, 5.000000000000000000 ) ) ;
#126262=ORIENTED_EDGE ( 'NONE', *, *, #58459, .F. ) ;
#126263=DIRECTION ( 'NONE',  ( -0.3543493200069162685, -0.000000000000000000, -0.9351131265310288487 ) ) ;
#126264=CARTESIAN_POINT ( 'NONE',  ( -34.92500000000001137, 22.22500000000000142, 4.000000000000000000 ) ) ;
#126265=CARTESIAN_POINT ( 'NONE',  ( 29.99451991528749417, 28.92564299267958816, 4.000000000000000000 ) ) ;
#126267=EDGE_LOOP ( 'NONE', ( #101545, #77334, #17695, #68763 ) ) ;
#126268=ADVANCED_FACE ( 'NONE', ( #125139 ), #69359, .T. ) ;
#126269=DIRECTION ( 'NONE',  ( -0.000000000000000000, 0.3543493200069153248, 0.9351131265310292928 ) ) ;
#126270=DIRECTION ( 'NONE',  ( 0.7071067811865487940, -0.7071067811865463515, 0.000000000000000000 ) ) ;
#126271=LINE ( 'NONE', #129115, #84427 ) ;
#126272=DIRECTION ( 'NONE',  ( 0.7071067811865487940, -0.7071067811865463515, 0.000000000000000000 ) ) ;
#126273=CARTESIAN_POINT ( 'NONE',  ( 48.18398860626899705, 28.73617430169820608, 5.000000000000000000 ) ) ;
#126276=CARTESIAN_POINT ( 'NONE',  ( -18.48921356237309510, -27.52281430457068367, 5.000000000000000000 ) ) ;
#126278=VERTEX_POINT ( 'NONE', #4016 ) ;
#126281=EDGE_LOOP ( 'NONE', ( #71186, #35161, #142277, #53361 ) ) ;
#126282=VERTEX_POINT ( 'NONE', #57067 ) ;
#126283=CARTESIAN_POINT ( 'NONE',  ( -34.49999999999975842, 15.43112307739202649, 4.000000000000000000 ) ) ;
#126284=CARTESIAN_POINT ( 'NONE',  ( -29.99451991528749417, 28.92564299267958816, 4.000000000000000000 ) ) ;
#126285=LINE ( 'NONE', #120657, #115528 ) ;
#126286=EDGE_LOOP ( 'NONE', ( #44013, #52112, #19557, #134762, #43135, #9498 ) ) ;
#126287=PLANE ( 'NONE',  #6242 ) ;
#126289=CARTESIAN_POINT ( 'NONE',  ( -14.01088028653938444, -22.02621442084248216, 4.990779571109223767 ) ) ;
#126291=ORIENTED_EDGE ( 'NONE', *, *, #95191, .F. ) ;
#126292=CARTESIAN_POINT ( 'NONE',  ( 34.49999999999975842, -12.08601207473285832, -10.46905243149102382 ) ) ;
#126293=ORIENTED_EDGE ( 'NONE', *, *, #128570, .F. ) ;
#126295=LINE ( 'NONE', #50177, #124062 ) ;
#126298=ORIENTED_EDGE ( 'NONE', *, *, #68226, .F. ) ;
#126300=CARTESIAN_POINT ( 'NONE',  ( -54.29974487139159578, -27.71228299555243879, 4.000000000000000000 ) ) ;
#126301=DIRECTION ( 'NONE',  ( -0.6830127018922180770, -0.6830127018922204085, -0.2588190451025214056 ) ) ;
#126302=PLANE ( 'NONE',  #1394 ) ;
#126303=VECTOR ( 'NONE', #101135, 999.9999999999998863 ) ;
#126304=ADVANCED_FACE ( 'NONE', ( #123744 ), #33869, .F. ) ;
#126306=ORIENTED_EDGE ( 'NONE', *, *, #5497, .T. ) ;
#126307=EDGE_CURVE ( 'NONE', #136490, #70384, #36021, .T. ) ;
#126309=DIRECTION ( 'NONE',  ( 0.7071067811865486830, -0.7071067811865464625, -0.000000000000000000 ) ) ;
#126311=EDGE_CURVE ( 'NONE', #21613, #127309, #78798, .T. ) ;
#126313=EDGE_LOOP ( 'NONE', ( #140954, #121247, #129392, #30301, #143399, #35857 ) ) ;
#126314=PLANE ( 'NONE',  #2984 ) ;
#126316=EDGE_CURVE ( 'NONE', #51626, #25547, #16082, .T. ) ;
#126317=VECTOR ( 'NONE', #91152, 1000.000000000000000 ) ;
#126318=CARTESIAN_POINT ( 'NONE',  ( -54.48921356237310221, -27.52281430457093236, 5.000000000000000000 ) ) ;
#126319=ORIENTED_EDGE ( 'NONE', *, *, #11052, .T. ) ;
#126320=CARTESIAN_POINT ( 'NONE',  ( 25.49999999999982947, -2.173586137069107860, -4.605770156576055818 ) ) ;
#126321=EDGE_CURVE ( 'NONE', #27882, #2711, #68648, .T. ) ;
#126322=FACE_BOUND ( 'NONE', #12396, .T. ) ;
#126323=EDGE_CURVE ( 'NONE', #22070, #82317, #14237, .T. ) ;
#126325=DIRECTION ( 'NONE',  ( 0.6830127018922181881, 0.6830127018922202975, -0.2588190451025214056 ) ) ;
#126327=DIRECTION ( 'NONE',  ( 0.3543493200069162685, -0.000000000000000000, -0.9351131265310288487 ) ) ;
#126328=VERTEX_POINT ( 'NONE', #112145 ) ;
#126329=CARTESIAN_POINT ( 'NONE',  ( 63.29974487139158867, -27.71228299555250274, 4.000000000000000000 ) ) ;
#126330=EDGE_CURVE ( 'NONE', #138900, #85225, #122265, .T. ) ;
#126331=VECTOR ( 'NONE', #1266, 999.9999999999998863 ) ;
#126334=ORIENTED_EDGE ( 'NONE', *, *, #39238, .T. ) ;
#126336=VERTEX_POINT ( 'NONE', #34577 ) ;
#126337=VECTOR ( 'NONE', #11843, 1000.000000000000000 ) ;
#126338=CARTESIAN_POINT ( 'NONE',  ( -27.49816348513939701, -17.24070752338409918, 8.407044977365289995 ) ) ;
#126339=CARTESIAN_POINT ( 'NONE',  ( 15.19713381108422290, 7.733989266307781385, 4.000000000000000000 ) ) ;
#126340=EDGE_LOOP ( 'NONE', ( #43130, #118267, #104945, #112569 ) ) ;
#126341=CARTESIAN_POINT ( 'NONE',  ( -9.183988606268997046, 28.73617430169793607, 5.000000000000000000 ) ) ;
#126342=EDGE_CURVE ( 'NONE', #139694, #99063, #102694, .T. ) ;
#126344=DIRECTION ( 'NONE',  ( 1.000000000000000000, 0.000000000000000000, 0.000000000000000000 ) ) ;
#126345=DIRECTION ( 'NONE',  ( 0.6830127018922181881, 0.6830127018922202975, -0.2588190451025214056 ) ) ;
#126347=ORIENTED_EDGE ( 'NONE', *, *, #58409, .T. ) ;
#126348=ADVANCED_FACE ( 'NONE', ( #67201 ), #123012, .T. ) ;
#126349=ORIENTED_EDGE ( 'NONE', *, *, #71290, .T. ) ;
#126350=DIRECTION ( 'NONE',  ( 0.7071067811865486830, -0.7071067811865464625, -0.000000000000000000 ) ) ;
#126353=ORIENTED_EDGE ( 'NONE', *, *, #53650, .F. ) ;
#126354=ORIENTED_EDGE ( 'NONE', *, *, #89467, .T. ) ;
#126358=LINE ( 'NONE', #69888, #57905 ) ;
#126359=CARTESIAN_POINT ( 'NONE',  ( 27.29974487139158512, -27.71228299555225405, 4.000000000000000000 ) ) ;
#126361=LINE ( 'NONE', #115450, #61145 ) ;
#126362=ORIENTED_EDGE ( 'NONE', *, *, #41132, .T. ) ;
#126363=CARTESIAN_POINT ( 'NONE',  ( 12.79289321881337038, -8.240707523384196875, 5.000000000000000000 ) ) ;
#126364=CARTESIAN_POINT ( 'NONE',  ( -10.49999999999992539, -8.568876922607726598, 4.000000000000000000 ) ) ;
#126365=EDGE_CURVE ( 'NONE', #83058, #83926, #111398, .T. ) ;
#126366=DIRECTION ( 'NONE',  ( -0.7071067811865487940, 0.7071067811865463515, -0.000000000000000000 ) ) ;
#126367=DIRECTION ( 'NONE',  ( -0.7071067811865487940, 0.7071067811865463515, 0.000000000000000000 ) ) ;
#126368=ORIENTED_EDGE ( 'NONE', *, *, #124702, .T. ) ;
#126370=ORIENTED_EDGE ( 'NONE', *, *, #6308, .T. ) ;
#126371=CARTESIAN_POINT ( 'NONE',  ( -29.39513766812461171, 21.75929247661548516, 21.32995629748192812 ) ) ;
#126372=CARTESIAN_POINT ( 'NONE',  ( 57.48921356237308800, -27.52281430457095368, 5.000000000000000000 ) ) ;
#126373=DIRECTION ( 'NONE',  ( -0.000000000000000000, 0.000000000000000000, 1.000000000000000000 ) ) ;
#126376=EDGE_CURVE ( 'NONE', #116464, #35767, #12085, .T. ) ;
#126377=DIRECTION ( 'NONE',  ( -0.6830127018922180770, -0.6830127018922204085, -0.2588190451025213501 ) ) ;
#126378=CARTESIAN_POINT ( 'NONE',  ( 34.75611968250419181, 2.812934254707362580, 4.955485411084882053 ) ) ;
#126379=DIRECTION ( 'NONE',  ( -0.6830127018922181881, 0.6830127018922202975, -0.2588190451025214056 ) ) ;
#126380=ORIENTED_EDGE ( 'NONE', *, *, #6295, .T. ) ;
#126381=CARTESIAN_POINT ( 'NONE',  ( 65.99451991528749772, 28.92564299267984396, 4.000000000000000000 ) ) ;
#126382=DIRECTION ( 'NONE',  ( 0.7071067811865487940, 0.7071067811865463515, -0.000000000000000000 ) ) ;
#126385=LINE ( 'NONE', #84354, #131760 ) ;
#126386=VERTEX_POINT ( 'NONE', #138172 ) ;
#126387=EDGE_CURVE ( 'NONE', #120628, #91989, #116416, .T. ) ;
#126388=EDGE_CURVE ( 'NONE', #8796, #25047, #60652, .T. ) ;
#126389=VERTEX_POINT ( 'NONE', #93936 ) ;
#126391=FACE_OUTER_BOUND ( 'NONE', #30786, .T. ) ;
#126392=( BOUNDED_CURVE ( )  B_SPLINE_CURVE ( 3, ( #93150, #72880, #117035, #108996 ),
 .UNSPECIFIED., .F., .T. ) 
 B_SPLINE_CURVE_WITH_KNOTS ( ( 4, 4 ),
 ( 2.001653308786167429, 3.503810798801451742 ),
 .UNSPECIFIED. ) 
 CURVE ( )  GEOMETRIC_REPRESENTATION_ITEM ( )  RATIONAL_B_SPLINE_CURVE ( ( 1.000000000000000000, 0.8206354192515235013, 0.8206354192515235013, 1.000000000000000000 ) ) 
 REPRESENTATION_ITEM ( '' )  );
#126394=DIRECTION ( 'NONE',  ( -0.000000000000000000, 0.000000000000000000, 1.000000000000000000 ) ) ;
#126395=LINE ( 'NONE', #69933, #94720 ) ;
#126396=CARTESIAN_POINT ( 'NONE',  ( -53.99451991528749062, 28.92564299267975869, 4.000000000000000000 ) ) ;
#126397=DIRECTION ( 'NONE',  ( -0.3543493200069162685, -0.000000000000000000, -0.9351131265310288487 ) ) ;
#126398=VECTOR ( 'NONE', #49668, 1000.000000000000000 ) ;
#126399=EDGE_LOOP ( 'NONE', ( #126169, #117780, #56850, #102134 ) ) ;
#126400=DIRECTION ( 'NONE',  ( -0.7071067811865487940, 0.7071067811865463515, 0.000000000000000000 ) ) ;
#126401=LINE ( 'NONE', #115489, #28438 ) ;
#126402=CARTESIAN_POINT ( 'NONE',  ( 0.000000000000000000, 0.000000000000000000, 5.000000000000000000 ) ) ;
#126405=ORIENTED_EDGE ( 'NONE', *, *, #125989, .T. ) ;
#126406=DIRECTION ( 'NONE',  ( 0.7071067811865487940, -0.7071067811865463515, 0.000000000000000000 ) ) ;
#126408=VERTEX_POINT ( 'NONE', #28711 ) ;
#126409=AXIS2_PLACEMENT_3D ( 'NONE', #345, #47498, #24268 ) ;
#126410=ORIENTED_EDGE ( 'NONE', *, *, #15546, .T. ) ;
#126411=CARTESIAN_POINT ( 'NONE',  ( 3.328169399223507519, -15.74070752338412404, 4.000000000000000000 ) ) ;
#126412=LINE ( 'NONE', #136573, #99313 ) ;
#126413=PLANE ( 'NONE',  #9433 ) ;
#126414=DIRECTION ( 'NONE',  ( 0.6830127018922180770, -0.6830127018922204085, -0.2588190451025213501 ) ) ;
#126415=ADVANCED_FACE ( 'NONE', ( #82373 ), #62766, .F. ) ;
#126416=LINE ( 'NONE', #16202, #92738 ) ;
#126418=EDGE_LOOP ( 'NONE', ( #127108, #75250, #118297, #7631 ) ) ;
#126419=ADVANCED_FACE ( 'NONE', ( #104816 ), #48296, .F. ) ;
#126420=CARTESIAN_POINT ( 'NONE',  ( -42.48921356237308800, -27.52281430457085065, 5.000000000000000000 ) ) ;
#126422=CARTESIAN_POINT ( 'NONE',  ( 36.85005128541002506, -8.240707523384189770, 17.25253755692247637 ) ) ;
#126423=CARTESIAN_POINT ( 'NONE',  ( 6.489213562373093325, -27.52281430457059841, 5.000000000000000000 ) ) ;
#126426=VECTOR ( 'NONE', #97369, 1000.000000000000000 ) ;
#126427=DIRECTION ( 'NONE',  ( -0.3543493200069162685, -0.000000000000000000, -0.9351131265310288487 ) ) ;
#126428=EDGE_LOOP ( 'NONE', ( #111568, #116838, #71876, #31333 ) ) ;
#126429=ORIENTED_EDGE ( 'NONE', *, *, #64358, .F. ) ;
#126431=LINE ( 'NONE', #135217, #23920 ) ;
#126432=AXIS2_PLACEMENT_3D ( 'NONE', #96458, #95055, #29797 ) ;
#126433=PLANE ( 'NONE',  #16104 ) ;
#126434=CARTESIAN_POINT ( 'NONE',  ( 3.328169399223507519, -9.740707523384187994, 4.000000000000000000 ) ) ;
#126436=ORIENTED_EDGE ( 'NONE', *, *, #99995, .F. ) ;
#126437=ADVANCED_FACE ( 'NONE', ( #126552 ), #84521, .T. ) ;
#126439=CARTESIAN_POINT ( 'NONE',  ( 17.99451991528748351, 28.92564299267950645, 4.000000000000000000 ) ) ;
#126441=CARTESIAN_POINT ( 'NONE',  ( -78.48921356237309510, -27.52281430457109934, 5.000000000000000000 ) ) ;
#126442=VERTEX_POINT ( 'NONE', #117801 ) ;
#126443=ORIENTED_EDGE ( 'NONE', *, *, #84173, .T. ) ;
#126444=DIRECTION ( 'NONE',  ( -0.7071067811865486830, -0.7071067811865464625, 0.000000000000000000 ) ) ;
#126445=CARTESIAN_POINT ( 'NONE',  ( 28.49999999999979750, -6.839392718269103888, -8.480912228396153552 ) ) ;
#126446=DIRECTION ( 'NONE',  ( -0.000000000000000000, 0.000000000000000000, 1.000000000000000000 ) ) ;
#126447=CARTESIAN_POINT ( 'NONE',  ( -63.48921356237309510, -27.52281430457099631, 5.000000000000000000 ) ) ;
#126448=CARTESIAN_POINT ( 'NONE',  ( 23.42930023009006391, -22.22500000000000142, 27.11262575547401354 ) ) ;
#126449=DIRECTION ( 'NONE',  ( -0.7071067811865487940, 0.7071067811865463515, -0.000000000000000000 ) ) ;
#126450=ORIENTED_EDGE ( 'NONE', *, *, #62774, .T. ) ;
#126451=LINE ( 'NONE', #105412, #106237 ) ;
#126453=LINE ( 'NONE', #127922, #47176 ) ;
#126454=CARTESIAN_POINT ( 'NONE',  ( 8.292986735706890045, -21.74070752338406365, 4.999753212805221558 ) ) ;
#126455=EDGE_LOOP ( 'NONE', ( #49408, #100230, #87557 ) ) ;
#126456=EDGE_CURVE ( 'NONE', #90217, #126591, #39588, .T. ) ;
#126457=ORIENTED_EDGE ( 'NONE', *, *, #115791, .F. ) ;
#126458=PLANE ( 'NONE',  #140278 ) ;
#126461=CARTESIAN_POINT ( 'NONE',  ( -0.3281693992235254487, 2.259292476615696099, 4.000000000000000000 ) ) ;
#126462=PLANE ( 'NONE',  #140404 ) ;
#126463=CARTESIAN_POINT ( 'NONE',  ( -34.75611968250420603, 14.81293425470721736, 4.955485411084898040 ) ) ;
#126464=ORIENTED_EDGE ( 'NONE', *, *, #5743, .T. ) ;
#126465=ORIENTED_EDGE ( 'NONE', *, *, #91607, .T. ) ;
#126467=DIRECTION ( 'NONE',  ( 0.6830127018922180770, -0.6830127018922204085, -0.2588190451025213501 ) ) ;
#126469=ORIENTED_EDGE ( 'NONE', *, *, #71045, .T. ) ;
#126470=EDGE_CURVE ( 'NONE', #101316, #6765, #81674, .T. ) ;
#126471=EDGE_CURVE ( 'NONE', #91252, #130600, #83822, .T. ) ;
#126472=ORIENTED_EDGE ( 'NONE', *, *, #58767, .F. ) ;
#126473=FACE_OUTER_BOUND ( 'NONE', #1012, .T. ) ;
#126474=ORIENTED_EDGE ( 'NONE', *, *, #26801, .F. ) ;
#126475=FACE_OUTER_BOUND ( 'NONE', #75033, .T. ) ;
#126476=LINE ( 'NONE', #16262, #79545 ) ;
#126477=VECTOR ( 'NONE', #112001, 1000.000000000000000 ) ;
#126478=EDGE_CURVE ( 'NONE', #19726, #82267, #59905, .T. ) ;
#126479=FACE_BOUND ( 'NONE', #142589, .T. ) ;
#126480=EDGE_CURVE ( 'NONE', #115809, #16774, #70771, .T. ) ;
#126481=FACE_OUTER_BOUND ( 'NONE', #138196, .T. ) ;
#126482=LINE ( 'NONE', #82302, #125377 ) ;
#126483=DIRECTION ( 'NONE',  ( -0.000000000000000000, 0.000000000000000000, 1.000000000000000000 ) ) ;
#126484=CARTESIAN_POINT ( 'NONE',  ( 23.51078643762690490, -27.52281430457038880, 5.000000000000000000 ) ) ;
#126486=EDGE_CURVE ( 'NONE', #99762, #129679, #83077, .T. ) ;
#126488=ORIENTED_EDGE ( 'NONE', *, *, #112206, .F. ) ;
#126493=CARTESIAN_POINT ( 'NONE',  ( 53.99451991528749062, 28.92564299267975869, 4.000000000000000000 ) ) ;
#126494=LINE ( 'NONE', #81607, #113824 ) ;
#126495=EDGE_CURVE ( 'NONE', #3029, #42047, #40312, .T. ) ;
#126496=LINE ( 'NONE', #83760, #117279 ) ;
#126497=DIRECTION ( 'NONE',  ( -0.6830127018922180770, -0.6830127018922204085, -0.2588190451025213501 ) ) ;
#126499=CARTESIAN_POINT ( 'NONE',  ( 47.99451991528749062, 28.92564299267971251, 4.000000000000000000 ) ) ;
#126500=LINE ( 'NONE', #61318, #142654 ) ;
#126501=VECTOR ( 'NONE', #101906, 1000.000000000000000 ) ;
#126502=CARTESIAN_POINT ( 'NONE',  ( -18.81246187583933960, -22.22500000000000142, 4.000000000000000000 ) ) ;
#126503=CARTESIAN_POINT ( 'NONE',  ( 11.99451991528749417, 28.92564299267946382, 4.000000000000000000 ) ) ;
#126504=LINE ( 'NONE', #60594, #130727 ) ;
#126505=CARTESIAN_POINT ( 'NONE',  ( -26.99451991528749417, 28.92564299267956685, 4.000000000000000000 ) ) ;
#126507=ADVANCED_FACE ( 'NONE', ( #33014 ), #131580, .T. ) ;
#126508=LINE ( 'NONE', #139583, #81651 ) ;
#126512=VERTEX_POINT ( 'NONE', #109819 ) ;
#126513=VECTOR ( 'NONE', #17693, 1000.000000000000000 ) ;
#126514=ORIENTED_EDGE ( 'NONE', *, *, #99440, .F. ) ;
#126515=ORIENTED_EDGE ( 'NONE', *, *, #113838, .T. ) ;
#126516=EDGE_CURVE ( 'NONE', #96047, #127352, #75781, .T. ) ;
#126518=EDGE_CURVE ( 'NONE', #50562, #18398, #120671, .T. ) ;
#126520=VECTOR ( 'NONE', #25195, 1000.000000000000114 ) ;
#126521=AXIS2_PLACEMENT_3D ( 'NONE', #48209, #59132, #14854 ) ;
#126522=EDGE_CURVE ( 'NONE', #119795, #72522, #121397, .T. ) ;
#126526=ORIENTED_EDGE ( 'NONE', *, *, #87394, .T. ) ;
#126527=DIRECTION ( 'NONE',  ( -0.7071067811865486830, -0.7071067811865464625, 0.000000000000000000 ) ) ;
#126528=VERTEX_POINT ( 'NONE', #22079 ) ;
#126529=FACE_OUTER_BOUND ( 'NONE', #26533, .T. ) ;
#126530=VECTOR ( 'NONE', #85089, 1000.000000000000000 ) ;
#126531=DIRECTION ( 'NONE',  ( 0.7071067811865487940, -0.7071067811865463515, 0.000000000000000000 ) ) ;
#126532=DIRECTION ( 'NONE',  ( -0.7071067811865486830, 0.7071067811865464625, 0.000000000000000000 ) ) ;
#126533=ORIENTED_EDGE ( 'NONE', *, *, #7980, .T. ) ;
#126534=VERTEX_POINT ( 'NONE', #98925 ) ;
#126535=DIRECTION ( 'NONE',  ( -0.7071067811865486830, -0.7071067811865464625, -0.000000000000000000 ) ) ;
#126536=CARTESIAN_POINT ( 'NONE',  ( -23.99451991528749062, 28.92564299267954908, 4.000000000000000000 ) ) ;
#126537=ORIENTED_EDGE ( 'NONE', *, *, #51157, .T. ) ;
#126538=CARTESIAN_POINT ( 'NONE',  ( -14.99999999999989519, -10.77435723561696435, -9.972017380717193902 ) ) ;
#126540=ORIENTED_EDGE ( 'NONE', *, *, #116509, .F. ) ;
#126541=VERTEX_POINT ( 'NONE', #32270 ) ;
#126542=ORIENTED_EDGE ( 'NONE', *, *, #104473, .T. ) ;
#126543=CARTESIAN_POINT ( 'NONE',  ( 30.18398860626900060, 28.73617430169808173, 5.000000000000000000 ) ) ;
#126544=DIRECTION ( 'NONE',  ( 0.6830127018922181881, 0.6830127018922202975, -0.2588190451025214056 ) ) ;
#126545=DIRECTION ( 'NONE',  ( 0.6830127018922181881, 0.6830127018922202975, -0.2588190451025214056 ) ) ;
#126546=CARTESIAN_POINT ( 'NONE',  ( 2.999999999999981792, -13.97847968911260175, -0.1324546996126730880 ) ) ;
#126547=DIRECTION ( 'NONE',  ( -0.3543493200069162685, -0.000000000000000000, -0.9351131265310288487 ) ) ;
#126548=ORIENTED_EDGE ( 'NONE', *, *, #57658, .F. ) ;
#126549=CARTESIAN_POINT ( 'NONE',  ( 13.17183060077637968, 9.759292476615621936, 4.000000000000000000 ) ) ;
#126551=LINE ( 'NONE', #18489, #50881 ) ;
#126552=FACE_OUTER_BOUND ( 'NONE', #23551, .T. ) ;
#126553=CARTESIAN_POINT ( 'NONE',  ( -11.70025512860841133, -27.71228299555198049, 4.000000000000000000 ) ) ;
#126554=ORIENTED_EDGE ( 'NONE', *, *, #947, .F. ) ;
#126555=VERTEX_POINT ( 'NONE', #66340 ) ;
#126556=EDGE_CURVE ( 'NONE', #93730, #58304, #20652, .T. ) ;
#126557=VERTEX_POINT ( 'NONE', #51892 ) ;
#126558=DIRECTION ( 'NONE',  ( 0.7071067811865487940, 0.7071067811865463515, -0.000000000000000000 ) ) ;
#126559=CARTESIAN_POINT ( 'NONE',  ( -15.48921356237309510, -27.52281430457066236, 5.000000000000000000 ) ) ;
#126560=CARTESIAN_POINT ( 'NONE',  ( 54.48921356237310221, -27.52281430457093236, 5.000000000000000000 ) ) ;
#126561=VECTOR ( 'NONE', #70354, 1000.000000000000000 ) ;
#126562=LINE ( 'NONE', #14247, #137727 ) ;
#126563=CARTESIAN_POINT ( 'NONE',  ( 28.49999999999981171, 19.46639925780206326, 5.000000000000000000 ) ) ;
#126565=CARTESIAN_POINT ( 'NONE',  ( 0.000000000000000000, 0.000000000000000000, 5.000000000000000000 ) ) ;
#126567=LINE ( 'NONE', #61386, #107980 ) ;
#126568=CARTESIAN_POINT ( 'NONE',  ( 34.92499999999998295, 22.22500000000000142, 4.500000000000000888 ) ) ;
#126569=CARTESIAN_POINT ( 'NONE',  ( 24.72281430457042717, -21.72500000000000142, 5.000000000000000000 ) ) ;
#126570=VECTOR ( 'NONE', #53121, 1000.000000000000227 ) ;
#126571=ORIENTED_EDGE ( 'NONE', *, *, #40746, .T. ) ;
#126573=ORIENTED_EDGE ( 'NONE', *, *, #123901, .T. ) ;
#126574=CARTESIAN_POINT ( 'NONE',  ( -23.99999999999983302, -19.06887692260762179, 4.000000000000000000 ) ) ;
#126575=CARTESIAN_POINT ( 'NONE',  ( -16.49999999999987566, -11.94781430457070392, 5.000000000000000000 ) ) ;
#126577=VECTOR ( 'NONE', #3614, 1000.000000000000227 ) ;
#126578=ADVANCED_FACE ( 'NONE', ( #65654 ), #140308, .F. ) ;
#126579=FACE_OUTER_BOUND ( 'NONE', #2715, .T. ) ;
#126580=CARTESIAN_POINT ( 'NONE',  ( -10.80981832425544731, -18.74070752338408852, 7.910009926591535567 ) ) ;
#126581=VERTEX_POINT ( 'NONE', #9782 ) ;
#126582=EDGE_CURVE ( 'NONE', #74261, #20046, #85196, .T. ) ;
#126586=ORIENTED_EDGE ( 'NONE', *, *, #19330, .F. ) ;
#126587=DIRECTION ( 'NONE',  ( 0.3543493200069162685, -0.000000000000000000, -0.9351131265310288487 ) ) ;
#126589=CARTESIAN_POINT ( 'NONE',  ( 21.81349135397625361, -15.74070752338412049, 8.904080028138892544 ) ) ;
#126591=VERTEX_POINT ( 'NONE', #30105 ) ;
#126593=ADVANCED_FACE ( 'NONE', ( #74354 ), #10486, .F. ) ;
#126594=CARTESIAN_POINT ( 'NONE',  ( 34.49999999999975842, -17.94567065516886117, 4.994342998332151673 ) ) ;
#126595=CARTESIAN_POINT ( 'NONE',  ( -16.49999999999988276, 14.14708470758589520, -0.5283514160166185025 ) ) ;
#126597=CARTESIAN_POINT ( 'NONE',  ( -18.18398860626898994, 28.73617430169800002, 5.000000000000000000 ) ) ;
#126599=ORIENTED_EDGE ( 'NONE', *, *, #133361, .F. ) ;
#126602=ORIENTED_EDGE ( 'NONE', *, *, #94146, .F. ) ;
#126604=LINE ( 'NONE', #103422, #107918 ) ;
#126605=CARTESIAN_POINT ( 'NONE',  ( 53.99451991528749062, 28.92564299267975869, 4.000000000000000000 ) ) ;
#126606=CARTESIAN_POINT ( 'NONE',  ( 0.1839886062690032631, 28.73617430169787568, 5.000000000000000000 ) ) ;
#126607=ORIENTED_EDGE ( 'NONE', *, *, #67562, .T. ) ;
#126608=ADVANCED_FACE ( 'NONE', ( #54052 ), #9020, .F. ) ;
#126609=DIRECTION ( 'NONE',  ( 0.7071067811865486830, -0.7071067811865464625, -0.000000000000000000 ) ) ;
#126611=AXIS2_PLACEMENT_3D ( 'NONE', #11089, #206, #101698 ) ;
#126614=CARTESIAN_POINT ( 'NONE',  ( -25.49999999999982236, -19.91253812416055524, 4.000000000000000000 ) ) ;
#126615=ORIENTED_EDGE ( 'NONE', *, *, #7175, .T. ) ;
#126616=DIRECTION ( 'NONE',  ( -0.7071067811865487940, 0.7071067811865463515, 0.000000000000000000 ) ) ;
#126617=CARTESIAN_POINT ( 'NONE',  ( -20.01088028653933648, -22.02621442084248216, 4.990779571109221102 ) ) ;
#126618=AXIS2_PLACEMENT_3D ( 'NONE', #53202, #119863, #64821 ) ;
#126619=CARTESIAN_POINT ( 'NONE',  ( 27.79289321881325847, 18.75929247661552779, 5.000000000000000000 ) ) ;
#126620=VECTOR ( 'NONE', #92781, 1000.000000000000000 ) ;
#126621=EDGE_LOOP ( 'NONE', ( #44304, #49870, #103482, #52979 ) ) ;
#126622=VERTEX_POINT ( 'NONE', #53284 ) ;
#126623=ORIENTED_EDGE ( 'NONE', *, *, #32833, .F. ) ;
#126624=VECTOR ( 'NONE', #22282, 1000.000000000000227 ) ;
#126626=EDGE_LOOP ( 'NONE', ( #70223, #59172, #138191 ) ) ;
#126627=DIRECTION ( 'NONE',  ( -1.000000000000000000, 0.000000000000000000, -0.000000000000000000 ) ) ;
#126628=EDGE_CURVE ( 'NONE', #91076, #108780, #21392, .T. ) ;
#126630=CARTESIAN_POINT ( 'NONE',  ( 74.99451991528749772, 28.92564299267990435, 4.000000000000000000 ) ) ;
#126631=DIRECTION ( 'NONE',  ( -0.3543493200069162685, -0.000000000000000000, -0.9351131265310288487 ) ) ;
#126632=VECTOR ( 'NONE', #13219, 999.9999999999998863 ) ;
#126633=DIRECTION ( 'NONE',  ( -0.7071067811865486830, -0.7071067811865464625, -0.000000000000000000 ) ) ;
#126634=ORIENTED_EDGE ( 'NONE', *, *, #132793, .F. ) ;
#126636=CARTESIAN_POINT ( 'NONE',  ( 28.49999999999980460, 9.431123077392088661, 4.000000000000000000 ) ) ;
#126637=EDGE_CURVE ( 'NONE', #113440, #128877, #96755, .T. ) ;
#126638=ADVANCED_FACE ( 'NONE', ( #119942 ), #97496, .T. ) ;
#126639=ORIENTED_EDGE ( 'NONE', *, *, #108245, .T. ) ;
#126641=DIRECTION ( 'NONE',  ( -0.7071067811865486830, 0.7071067811865464625, 0.000000000000000000 ) ) ;
#126642=CARTESIAN_POINT ( 'NONE',  ( -30.48921356237309510, -27.52281430457076894, 5.000000000000000000 ) ) ;
#126643=EDGE_CURVE ( 'NONE', #1086, #58487, #31555, .T. ) ;
#126644=( BOUNDED_CURVE ( )  B_SPLINE_CURVE ( 3, ( #115533, #39466, #28585, #27850 ),
 .UNSPECIFIED., .F., .F. ) 
 B_SPLINE_CURVE_WITH_KNOTS ( ( 4, 4 ),
 ( 1.964434688349484537, 3.503810798801452187 ),
 .UNSPECIFIED. ) 
 CURVE ( )  GEOMETRIC_REPRESENTATION_ITEM ( )  RATIONAL_B_SPLINE_CURVE ( ( 1.000000000000000000, 0.8120851936182271746, 0.8120851936182271746, 1.000000000000000000 ) ) 
 REPRESENTATION_ITEM ( '' )  );
#126645=ORIENTED_EDGE ( 'NONE', *, *, #94161, .T. ) ;
#126646=VERTEX_POINT ( 'NONE', #57609 ) ;
#126647=CARTESIAN_POINT ( 'NONE',  ( 21.06011071044006755, -9.740707523384187994, 10.89222023123375926 ) ) ;
#126648=ADVANCED_FACE ( 'NONE', ( #80778 ), #102538, .F. ) ;
#126649=EDGE_CURVE ( 'NONE', #129256, #94995, #45318, .T. ) ;
#126650=CARTESIAN_POINT ( 'NONE',  ( -26.99999999999981171, -11.35517001088074807, -1.126524801160169620 ) ) ;
#126652=DIRECTION ( 'NONE',  ( 0.7071067811865487940, 0.7071067811865463515, -0.000000000000000000 ) ) ;
#126653=DIRECTION ( 'NONE',  ( -0.000000000000000000, 0.3543493200069153248, 0.9351131265310292928 ) ) ;
#126654=VECTOR ( 'NONE', #14911, 1000.000000000000000 ) ;
#126655=PLANE ( 'NONE',  #136778 ) ;
#126658=ORIENTED_EDGE ( 'NONE', *, *, #63655, .T. ) ;
#126659=ORIENTED_EDGE ( 'NONE', *, *, #43394, .F. ) ;
#126660=ORIENTED_EDGE ( 'NONE', *, *, #11070, .T. ) ;
#126661=EDGE_CURVE ( 'NONE', #68252, #8528, #25658, .T. ) ;
#126662=ORIENTED_EDGE ( 'NONE', *, *, #64624, .T. ) ;
#126663=VECTOR ( 'NONE', #89738, 1000.000000000000000 ) ;
#126664=ADVANCED_FACE ( 'NONE', ( #22764 ), #122109, .T. ) ;
#126665=DIRECTION ( 'NONE',  ( -0.000000000000000000, -0.3543493200069152693, 0.9351131265310292928 ) ) ;
#126667=ORIENTED_EDGE ( 'NONE', *, *, #140060, .T. ) ;
#126668=PLANE ( 'NONE',  #92243 ) ;
#126669=FACE_OUTER_BOUND ( 'NONE', #125663, .T. ) ;
#126671=AXIS2_PLACEMENT_3D ( 'NONE', #66546, #33924, #1940 ) ;
#126672=FACE_OUTER_BOUND ( 'NONE', #58185, .T. ) ;
#126673=DIRECTION ( 'NONE',  ( 0.7071067811865486830, -0.7071067811865464625, -0.000000000000000000 ) ) ;
#126674=ORIENTED_EDGE ( 'NONE', *, *, #52476, .T. ) ;
#126675=CARTESIAN_POINT ( 'NONE',  ( 21.18398860626899349, 28.73617430169802134, 5.000000000000000000 ) ) ;
#126676=CARTESIAN_POINT ( 'NONE',  ( 35.99451991528749772, 28.92564299267963079, 4.000000000000000000 ) ) ;
#126678=CARTESIAN_POINT ( 'NONE',  ( -32.28242261357410570, -21.73023691814492508, 5.000000000000000888 ) ) ;
#126679=ORIENTED_EDGE ( 'NONE', *, *, #31105, .T. ) ;
#126680=VERTEX_POINT ( 'NONE', #101796 ) ;
#126681=CARTESIAN_POINT ( 'NONE',  ( 29.99451991528749417, 28.92564299267958816, 4.000000000000000000 ) ) ;
#126683=VERTEX_POINT ( 'NONE', #56904 ) ;
#126685=ORIENTED_EDGE ( 'NONE', *, *, #142873, .T. ) ;
#126686=EDGE_CURVE ( 'NONE', #55719, #141993, #11175, .T. ) ;
#126688=EDGE_CURVE ( 'NONE', #3304, #70500, #77921, .T. ) ;
#126689=DIRECTION ( 'NONE',  ( -0.6830127018922180770, -0.6830127018922204085, -0.2588190451025213501 ) ) ;
#126690=VECTOR ( 'NONE', #100831, 1000.000000000000000 ) ;
#126692=PLANE ( 'NONE',  #70352 ) ;
#126694=DIRECTION ( 'NONE',  ( 0.7071067811865487940, 0.7071067811865463515, 0.000000000000000000 ) ) ;
#126696=PLANE ( 'NONE',  #49365 ) ;
#126698=CARTESIAN_POINT ( 'NONE',  ( -12.48921356237309155, -27.52281430457064104, 5.000000000000000000 ) ) ;
#126699=ORIENTED_EDGE ( 'NONE', *, *, #3985, .F. ) ;
#126701=PLANE ( 'NONE',  #49893 ) ;
#126702=VERTEX_POINT ( 'NONE', #55452 ) ;
#126705=ORIENTED_EDGE ( 'NONE', *, *, #39914, .F. ) ;
#126706=FACE_OUTER_BOUND ( 'NONE', #34249, .T. ) ;
#126708=CARTESIAN_POINT ( 'NONE',  ( -21.48921356237309155, -27.52281430457070499, 5.000000000000000000 ) ) ;
#126709=FACE_OUTER_BOUND ( 'NONE', #139368, .T. ) ;
#126710=FACE_OUTER_BOUND ( 'NONE', #43280, .T. ) ;
#126711=ORIENTED_EDGE ( 'NONE', *, *, #53288, .T. ) ;
#126713=VERTEX_POINT ( 'NONE', #99641 ) ;
#126714=VECTOR ( 'NONE', #3463, 1000.000000000000000 ) ;
#126716=CARTESIAN_POINT ( 'NONE',  ( -9.299744871391588674, -27.71228299555212971, 4.000000000000000000 ) ) ;
#126718=CARTESIAN_POINT ( 'NONE',  ( 23.99451991528749062, 28.92564299267954908, 4.000000000000000000 ) ) ;
#126719=CARTESIAN_POINT ( 'NONE',  ( -27.48921356237309155, -27.52281430457074762, 5.000000000000000000 ) ) ;
#126720=DIRECTION ( 'NONE',  ( 0.7071067811865487940, 0.7071067811865463515, 0.000000000000000000 ) ) ;
#126721=EDGE_LOOP ( 'NONE', ( #17987, #61813, #92238, #8068 ) ) ;
#126724=FACE_OUTER_BOUND ( 'NONE', #14258, .T. ) ;
#126725=CARTESIAN_POINT ( 'NONE',  ( -72.48921356237309510, -27.52281430457106026, 5.000000000000000000 ) ) ;
#126726=VECTOR ( 'NONE', #95440, 1000.000000000000000 ) ;
#126728=CARTESIAN_POINT ( 'NONE',  ( -56.99451991528749062, 28.92564299267978001, 4.000000000000000000 ) ) ;
#126729=FACE_OUTER_BOUND ( 'NONE', #96173, .T. ) ;
#126730=CARTESIAN_POINT ( 'NONE',  ( 21.70710678118640402, 20.25929247661551358, 5.000000000000000000 ) ) ;
#126731=PLANE ( 'NONE',  #9154 ) ;
#126732=DIRECTION ( 'NONE',  ( -0.7071067811865486830, -0.7071067811865464625, 0.000000000000000000 ) ) ;
#126733=CARTESIAN_POINT ( 'NONE',  ( -2.816011393730999401, 28.73617430169785436, 5.000000000000000000 ) ) ;
#126734=VERTEX_POINT ( 'NONE', #90949 ) ;
#126738=ADVANCED_FACE ( 'NONE', ( #13340 ), #312, .F. ) ;
#126739=DIRECTION ( 'NONE',  ( -0.7071067811865486830, -0.7071067811865464625, -0.000000000000000000 ) ) ;
#126740=DIRECTION ( 'NONE',  ( -0.000000000000000000, 0.000000000000000000, 1.000000000000000000 ) ) ;
#126741=ORIENTED_EDGE ( 'NONE', *, *, #67245, .T. ) ;
#126742=VERTEX_POINT ( 'NONE', #88806 ) ;
#126743=EDGE_CURVE ( 'NONE', #122527, #84994, #67042, .T. ) ;
#126744=EDGE_CURVE ( 'NONE', #667, #119248, #111225, .T. ) ;
#126745=DIRECTION ( 'NONE',  ( -0.000000000000000000, 0.3543493200069152138, -0.9351131265310292928 ) ) ;
#126746=DIRECTION ( 'NONE',  ( -0.000000000000000000, 0.3543493200069153248, 0.9351131265310292928 ) ) ;
#126747=CARTESIAN_POINT ( 'NONE',  ( 21.29974487139158512, -27.71228299555221142, 4.000000000000000000 ) ) ;
#126750=DIRECTION ( 'NONE',  ( -0.000000000000000000, 0.000000000000000000, 1.000000000000000000 ) ) ;
#126751=ORIENTED_EDGE ( 'NONE', *, *, #83066, .T. ) ;
#126752=EDGE_CURVE ( 'NONE', #7814, #5802, #58356, .T. ) ;
#126754=CARTESIAN_POINT ( 'NONE',  ( 18.29974487139159223, -27.71228299555219010, 4.000000000000000000 ) ) ;
#126757=VECTOR ( 'NONE', #115838, 1000.000000000000000 ) ;
#126758=DIRECTION ( 'NONE',  ( -0.7071067811865486830, 0.7071067811865464625, 0.000000000000000000 ) ) ;
#126759=( BOUNDED_CURVE ( )  B_SPLINE_CURVE ( 3, ( #143316, #99073, #11338, #88965 ),
 .UNSPECIFIED., .F., .T. ) 
 B_SPLINE_CURVE_WITH_KNOTS ( ( 4, 4 ),
 ( 5.143245962375961433, 6.645403452391247079 ),
 .UNSPECIFIED. ) 
 CURVE ( )  GEOMETRIC_REPRESENTATION_ITEM ( )  RATIONAL_B_SPLINE_CURVE ( ( 1.000000000000000000, 0.8206354192515231682, 0.8206354192515231682, 1.000000000000000000 ) ) 
 REPRESENTATION_ITEM ( '' )  );
#126760=CARTESIAN_POINT ( 'NONE',  ( 18.29974487139159223, -27.71228299555219010, 4.000000000000000000 ) ) ;
#126763=PLANE ( 'NONE',  #12463 ) ;
#126767=CARTESIAN_POINT ( 'NONE',  ( -39.48921356237310221, -27.52281430457082934, 5.000000000000000000 ) ) ;
#126768=CARTESIAN_POINT ( 'NONE',  ( -1.499999999999989120, 6.431123077392125964, 4.000000000000000000 ) ) ;
#126769=CARTESIAN_POINT ( 'NONE',  ( 57.18398860626899705, 28.73617430169827358, 5.000000000000000000 ) ) ;
#126771=EDGE_LOOP ( 'NONE', ( #138323, #38625, #91341, #114289 ) ) ;
#126773=EDGE_CURVE ( 'NONE', #13028, #136170, #80085, .T. ) ;
#126774=ORIENTED_EDGE ( 'NONE', *, *, #82314, .T. ) ;
#126775=ORIENTED_EDGE ( 'NONE', *, *, #13942, .F. ) ;
#126778=EDGE_CURVE ( 'NONE', #131518, #60169, #91640, .T. ) ;
#126779=LINE ( 'NONE', #36925, #2322 ) ;
#126780=LINE ( 'NONE', #94155, #103447 ) ;
#126781=ORIENTED_EDGE ( 'NONE', *, *, #135064, .F. ) ;
#126782=ADVANCED_FACE ( 'NONE', ( #56204 ), #100387, .F. ) ;
#126783=CARTESIAN_POINT ( 'NONE',  ( 5.700255128608413102, -27.71228299555201957, 4.000000000000000000 ) ) ;
#126784=CARTESIAN_POINT ( 'NONE',  ( 32.29298673570672662, -21.74070752338405654, 4.999753212805222446 ) ) ;
#126786=VECTOR ( 'NONE', #98360, 1000.000000000000000 ) ;
#126789=CARTESIAN_POINT ( 'NONE',  ( 16.49999999999988987, 18.05218569542898521, 5.000000000000000000 ) ) ;
#126790=EDGE_CURVE ( 'NONE', #17257, #116142, #134446, .T. ) ;
#126791=LINE ( 'NONE', #17328, #119287 ) ;
#126792=FACE_OUTER_BOUND ( 'NONE', #103398, .T. ) ;
#126793=DIRECTION ( 'NONE',  ( -0.3543493200069162685, -0.000000000000000000, -0.9351131265310288487 ) ) ;
#126794=LINE ( 'NONE', #100437, #68429 ) ;
#126796=ORIENTED_EDGE ( 'NONE', *, *, #81097, .T. ) ;
#126797=VERTEX_POINT ( 'NONE', #112674 ) ;
#126799=VECTOR ( 'NONE', #72909, 1000.000000000000227 ) ;
#126800=ORIENTED_EDGE ( 'NONE', *, *, #131769, .F. ) ;
#126801=ADVANCED_FACE ( 'NONE', ( #60471 ), #137298, .T. ) ;
#126802=DIRECTION ( 'NONE',  ( -0.6830127018922180770, -0.6830127018922204085, -0.2588190451025213501 ) ) ;
#126803=CARTESIAN_POINT ( 'NONE',  ( -75.29974487139158157, -27.71228299555258445, 4.000000000000000000 ) ) ;
#126804=ORIENTED_EDGE ( 'NONE', *, *, #54161, .F. ) ;
#126805=FACE_OUTER_BOUND ( 'NONE', #78063, .T. ) ;
#126806=PLANE ( 'NONE',  #14224 ) ;
#126807=EDGE_CURVE ( 'NONE', #114717, #58130, #3866, .T. ) ;
#126810=ORIENTED_EDGE ( 'NONE', *, *, #80351, .F. ) ;
#126811=ADVANCED_FACE ( 'NONE', ( #26395 ), #6011, .T. ) ;
#126812=LINE ( 'NONE', #45210, #69769 ) ;
#126813=ORIENTED_EDGE ( 'NONE', *, *, #72861, .T. ) ;
#126815=LINE ( 'NONE', #73885, #141813 ) ;
#126816=PLANE ( 'NONE',  #91758 ) ;
#126818=EDGE_CURVE ( 'NONE', #65462, #119206, #103908, .T. ) ;
#126819=ORIENTED_EDGE ( 'NONE', *, *, #36969, .F. ) ;
#126820=VERTEX_POINT ( 'NONE', #93780 ) ;
#126821=VECTOR ( 'NONE', #96000, 1000.000000000000000 ) ;
#126822=ORIENTED_EDGE ( 'NONE', *, *, #129122, .F. ) ;
#126825=VECTOR ( 'NONE', #67712, 1000.000000000000000 ) ;
#126826=CARTESIAN_POINT ( 'NONE',  ( -42.18398860626899705, 28.73617430169816700, 5.000000000000000000 ) ) ;
#126828=ORIENTED_EDGE ( 'NONE', *, *, #14377, .T. ) ;
#126830=EDGE_CURVE ( 'NONE', #127624, #139771, #138007, .T. ) ;
#126831=CARTESIAN_POINT ( 'NONE',  ( -13.27644930412397350, 4.689949953678146599, 5.000000000000000000 ) ) ;
#126833=EDGE_LOOP ( 'NONE', ( #111582, #7275, #78383, #34449 ) ) ;
#126836=CARTESIAN_POINT ( 'NONE',  ( 39.18398860626899705, 28.73617430169814568, 5.000000000000000000 ) ) ;
#126837=CARTESIAN_POINT ( 'NONE',  ( 39.48921356237310221, -27.52281430457082934, 5.000000000000000000 ) ) ;
#126838=ORIENTED_EDGE ( 'NONE', *, *, #11933, .T. ) ;
#126840=CARTESIAN_POINT ( 'NONE',  ( -22.82816939922337340, -14.24070752338413826, 4.000000000000000000 ) ) ;
#126841=EDGE_LOOP ( 'NONE', ( #85363, #84888, #18407 ) ) ;
#126842=CARTESIAN_POINT ( 'NONE',  ( -19.49999999999986500, 9.127013188829483425, 4.802533355213530086 ) ) ;
#126843=EDGE_CURVE ( 'NONE', #94488, #673, #127857, .T. ) ;
#126844=FACE_BOUND ( 'NONE', #106857, .T. ) ;
#126845=ORIENTED_EDGE ( 'NONE', *, *, #86590, .F. ) ;
#126847=CARTESIAN_POINT ( 'NONE',  ( 0.000000000000000000, 0.000000000000000000, 5.000000000000000000 ) ) ;
#126848=PLANE ( 'NONE',  #30695 ) ;
#126850=PLANE ( 'NONE',  #36597 ) ;
#126851=VERTEX_POINT ( 'NONE', #94476 ) ;
#126854=ORIENTED_EDGE ( 'NONE', *, *, #141353, .T. ) ;
#126857=ORIENTED_EDGE ( 'NONE', *, *, #82838, .F. ) ;
#126858=LINE ( 'NONE', #137777, #117880 ) ;
#126859=FACE_OUTER_BOUND ( 'NONE', #131983, .T. ) ;
#126862=EDGE_CURVE ( 'NONE', #20488, #3243, #114786, .T. ) ;
#126864=EDGE_CURVE ( 'NONE', #107481, #60758, #114105, .T. ) ;
#126865=CARTESIAN_POINT ( 'NONE',  ( -39.48921356237310221, -27.52281430457082934, 5.000000000000000000 ) ) ;
#126866=FACE_OUTER_BOUND ( 'NONE', #121135, .T. ) ;
#126867=DIRECTION ( 'NONE',  ( -0.6830127018922181881, 0.6830127018922202975, -0.2588190451025214056 ) ) ;
#126868=CARTESIAN_POINT ( 'NONE',  ( -34.42500000000001137, -16.45860074219782021, 5.000000000000000000 ) ) ;
#126870=ORIENTED_EDGE ( 'NONE', *, *, #3122, .T. ) ;
#126871=ORIENTED_EDGE ( 'NONE', *, *, #138615, .T. ) ;
#126872=VERTEX_POINT ( 'NONE', #59748 ) ;
#126874=ORIENTED_EDGE ( 'NONE', *, *, #129713, .F. ) ;
#126876=DIRECTION ( 'NONE',  ( 0.7071067811865487940, 0.7071067811865463515, 0.000000000000000000 ) ) ;
#126877=FACE_OUTER_BOUND ( 'NONE', #28280, .T. ) ;
#126878=EDGE_CURVE ( 'NONE', #137919, #72813, #37995, .T. ) ;
#126879=DIRECTION ( 'NONE',  ( 0.3543493200069162685, -0.000000000000000000, -0.9351131265310288487 ) ) ;
#126880=EDGE_LOOP ( 'NONE', ( #48459, #126334, #23724, #76533 ) ) ;
#126881=LINE ( 'NONE', #37039, #125125 ) ;
#126882=ORIENTED_EDGE ( 'NONE', *, *, #14340, .T. ) ;
#126883=LINE ( 'NONE', #18847, #32879 ) ;
#126884=LINE ( 'NONE', #4343, #102862 ) ;
#126886=EDGE_LOOP ( 'NONE', ( #101332, #30444, #72414, #89240 ) ) ;
#126888=CARTESIAN_POINT ( 'NONE',  ( 23.99999999999982947, -21.84840872380822674, 2.849755605029664185 ) ) ;
#126889=VECTOR ( 'NONE', #52519, 1000.000000000000227 ) ;
#126890=DIRECTION ( 'NONE',  ( 0.7071067811865487940, 0.7071067811865463515, 0.000000000000000000 ) ) ;
#126891=CARTESIAN_POINT ( 'NONE',  ( 36.48921356237310221, -27.52281430457080802, 5.000000000000000000 ) ) ;
#126892=ORIENTED_EDGE ( 'NONE', *, *, #139599, .T. ) ;
#126893=VERTEX_POINT ( 'NONE', #50289 ) ;
#126894=CARTESIAN_POINT ( 'NONE',  ( -38.99451991528749062, 28.92564299267965211, 4.000000000000000000 ) ) ;
#126897=DIRECTION ( 'NONE',  ( 0.7071067811865487940, 0.7071067811865463515, 0.000000000000000000 ) ) ;
#126898=DIRECTION ( 'NONE',  ( 0.7071067811865486830, -0.7071067811865464625, -0.000000000000000000 ) ) ;
#126899=CARTESIAN_POINT ( 'NONE',  ( -27.18398860626900060, 28.73617430169806042, 5.000000000000000000 ) ) ;
#126901=CARTESIAN_POINT ( 'NONE',  ( -4.968364840778061620, 2.259292476615697876, 13.77329220150635969 ) ) ;
#126902=LINE ( 'NONE', #50099, #18649 ) ;
#126903=LINE ( 'NONE', #136371, #79335 ) ;
#126904=EDGE_CURVE ( 'NONE', #81952, #35824, #126395, .T. ) ;
#126905=ORIENTED_EDGE ( 'NONE', *, *, #62455, .F. ) ;
#126906=DIRECTION ( 'NONE',  ( 0.7071067811865487940, 0.7071067811865463515, -0.000000000000000000 ) ) ;
#126907=AXIS2_PLACEMENT_3D ( 'NONE', #52890, #98561, #97094 ) ;
#126908=LINE ( 'NONE', #71872, #65586 ) ;
#126909=EDGE_CURVE ( 'NONE', #56401, #73002, #82224, .T. ) ;
#126910=ORIENTED_EDGE ( 'NONE', *, *, #94572, .F. ) ;
#126911=VECTOR ( 'NONE', #24331, 1000.000000000000000 ) ;
#126912=DIRECTION ( 'NONE',  ( 0.6830127018922180770, -0.6830127018922202975, -0.2588190451025213501 ) ) ;
#126913=ORIENTED_EDGE ( 'NONE', *, *, #125512, .F. ) ;
#126914=EDGE_CURVE ( 'NONE', #84947, #75086, #103214, .T. ) ;
#126915=EDGE_CURVE ( 'NONE', #38388, #102218, #71327, .T. ) ;
#126916=VERTEX_POINT ( 'NONE', #45075 ) ;
#126917=DIRECTION ( 'NONE',  ( 0.6830127018922180770, -0.6830127018922204085, -0.2588190451025213501 ) ) ;
#126919=VECTOR ( 'NONE', #129022, 999.9999999999998863 ) ;
#126920=ORIENTED_EDGE ( 'NONE', *, *, #139354, .F. ) ;
#126921=DIRECTION ( 'NONE',  ( 0.6830127018922181881, 0.6830127018922202975, -0.2588190451025214056 ) ) ;
#126922=VECTOR ( 'NONE', #12924, 999.9999999999998863 ) ;
#126923=EDGE_CURVE ( 'NONE', #73333, #61904, #111718, .T. ) ;
#126924=EDGE_CURVE ( 'NONE', #107783, #94758, #55928, .T. ) ;
#126925=DIRECTION ( 'NONE',  ( 0.7071067811865486830, -0.7071067811865464625, -0.000000000000000000 ) ) ;
#126926=CARTESIAN_POINT ( 'NONE',  ( -33.79289321881321939, 0.7592924766157086447, 5.000000000000000000 ) ) ;
#126928=EDGE_LOOP ( 'NONE', ( #22143, #114363, #94889, #62558 ) ) ;
#126929=LINE ( 'NONE', #6543, #138785 ) ;
#126930=CARTESIAN_POINT ( 'NONE',  ( -33.71757738642545377, -21.73023691814492864, 5.000000000000000888 ) ) ;
#126931=ADVANCED_FACE ( 'NONE', ( #113122 ), #134191, .T. ) ;
#126932=DIRECTION ( 'NONE',  ( -0.7071067811865486830, -0.7071067811865464625, 0.000000000000000000 ) ) ;
#126935=CARTESIAN_POINT ( 'NONE',  ( 0.000000000000000000, 0.000000000000000000, 5.000000000000000000 ) ) ;
#126936=VECTOR ( 'NONE', #100208, 1000.000000000000114 ) ;
#126937=DIRECTION ( 'NONE',  ( -0.3543493200069163240, 0.000000000000000000, 0.9351131265310288487 ) ) ;
#126938=EDGE_CURVE ( 'NONE', #34187, #16081, #68949, .T. ) ;
#126939=CARTESIAN_POINT ( 'NONE',  ( 75.48921356237309510, -27.52281430457107803, 5.000000000000000000 ) ) ;
#126940=CARTESIAN_POINT ( 'NONE',  ( 34.49999999999975842, -2.173586137069107860, -4.605770156576030949 ) ) ;
#126941=ORIENTED_EDGE ( 'NONE', *, *, #4857, .F. ) ;
#126942=VERTEX_POINT ( 'NONE', #782 ) ;
#126943=ORIENTED_EDGE ( 'NONE', *, *, #51510, .T. ) ;
#126946=VECTOR ( 'NONE', #91831, 1000.000000000000000 ) ;
#126947=VERTEX_POINT ( 'NONE', #122571 ) ;
#126948=ORIENTED_EDGE ( 'NONE', *, *, #59069, .F. ) ;
#126950=AXIS2_PLACEMENT_3D ( 'NONE', #65690, #9820, #1064 ) ;
#126951=CARTESIAN_POINT ( 'NONE',  ( 0.000000000000000000, 0.000000000000000000, 5.000000000000000000 ) ) ;
#126952=EDGE_LOOP ( 'NONE', ( #5631, #122309, #14743, #79935 ) ) ;
#126953=DIRECTION ( 'NONE',  ( -0.7071067811865487940, 0.7071067811865463515, -0.000000000000000000 ) ) ;
#126954=VECTOR ( 'NONE', #20650, 1000.000000000000000 ) ;
#126955=EDGE_CURVE ( 'NONE', #61664, #77672, #12385, .T. ) ;
#126956=CARTESIAN_POINT ( 'NONE',  ( -50.99451991528749062, 28.92564299267973738, 4.000000000000000000 ) ) ;
#126958=LINE ( 'NONE', #17489, #34747 ) ;
#126959=CARTESIAN_POINT ( 'NONE',  ( -27.48921356237309155, -27.52281430457074762, 5.000000000000000000 ) ) ;
#126961=VERTEX_POINT ( 'NONE', #89939 ) ;
#126963=DIRECTION ( 'NONE',  ( 0.7071067811865486830, -0.7071067811865464625, -0.000000000000000000 ) ) ;
#126964=CARTESIAN_POINT ( 'NONE',  ( 25.49999999999983658, 19.08746187583905041, 4.000000000000000000 ) ) ;
#126965=DIRECTION ( 'NONE',  ( -1.000000000000000000, 0.000000000000000000, 0.000000000000000000 ) ) ;
#126966=EDGE_CURVE ( 'NONE', #17946, #134862, #78380, .T. ) ;
#126967=CARTESIAN_POINT ( 'NONE',  ( -42.18398860626899705, 28.73617430169816700, 5.000000000000000000 ) ) ;
#126968=CARTESIAN_POINT ( 'NONE',  ( -48.18398860626899705, 28.73617430169820608, 5.000000000000000000 ) ) ;
#126970=PLANE ( 'NONE',  #37461 ) ;
#126971=CARTESIAN_POINT ( 'NONE',  ( -69.18398860626899705, 28.73617430169835529, 5.000000000000000000 ) ) ;
#126972=EDGE_LOOP ( 'NONE', ( #51965, #75751, #85949, #8073 ) ) ;
#126973=VERTEX_POINT ( 'NONE', #81249 ) ;
#126975=ORIENTED_EDGE ( 'NONE', *, *, #129093, .F. ) ;
#126976=CARTESIAN_POINT ( 'NONE',  ( 5.816011393731002066, 28.73617430169783304, 5.000000000000000000 ) ) ;
#126977=CARTESIAN_POINT ( 'NONE',  ( -20.99451991528748707, 28.92564299267952777, 4.000000000000000000 ) ) ;
#126978=ORIENTED_EDGE ( 'NONE', *, *, #118474, .T. ) ;
#126979=VECTOR ( 'NONE', #128331, 1000.000000000000227 ) ;
#126980=DIRECTION ( 'NONE',  ( 0.7071067811865487940, -0.7071067811865463515, 0.000000000000000000 ) ) ;
#126981=DIRECTION ( 'NONE',  ( 0.6830127018922180770, -0.6830127018922204085, -0.2588190451025213501 ) ) ;
#126982=VECTOR ( 'NONE', #118375, 1000.000000000000000 ) ;
#126983=DIRECTION ( 'NONE',  ( 0.7071067811865486830, -0.7071067811865464625, -0.000000000000000000 ) ) ;
#126984=CARTESIAN_POINT ( 'NONE',  ( -33.18398860626899705, 28.73617430169810305, 5.000000000000000000 ) ) ;
#126985=EDGE_CURVE ( 'NONE', #45188, #13042, #134929, .T. ) ;
#126987=ORIENTED_EDGE ( 'NONE', *, *, #103217, .F. ) ;
#126988=ADVANCED_FACE ( 'NONE', ( #133475 ), #70405, .T. ) ;
#126989=DIRECTION ( 'NONE',  ( 0.7071067811865487940, 0.7071067811865463515, 0.000000000000000000 ) ) ;
#126990=ORIENTED_EDGE ( 'NONE', *, *, #93063, .F. ) ;
#126991=CARTESIAN_POINT ( 'NONE',  ( 17.99999999999987566, 14.87792677143811026, -11.06722581663436067 ) ) ;
#126993=CARTESIAN_POINT ( 'NONE',  ( 11.99999999999991296, 18.08204922493374056, 0.9627537363044594843 ) ) ;
#126994=EDGE_CURVE ( 'NONE', #124430, #88917, #57359, .T. ) ;
#126995=CARTESIAN_POINT ( 'NONE',  ( 1.499999999999990896, -5.568876922607761237, 4.000000000000000000 ) ) ;
#126996=EDGE_LOOP ( 'NONE', ( #96877, #75542, #75195, #21577 ) ) ;
#126998=EDGE_LOOP ( 'NONE', ( #129893, #68284, #143325, #51151 ) ) ;
#126999=CARTESIAN_POINT ( 'NONE',  ( 10.17183060077640810, 15.75929247661557042, 4.000000000000000000 ) ) ;
#127000=FACE_OUTER_BOUND ( 'NONE', #120138, .T. ) ;
#127001=DIRECTION ( 'NONE',  ( -0.3543493200069162685, -0.000000000000000000, -0.9351131265310288487 ) ) ;
#127002=CARTESIAN_POINT ( 'NONE',  ( 39.18398860626899705, 28.73617430169814568, 5.000000000000000000 ) ) ;
#127004=VERTEX_POINT ( 'NONE', #69667 ) ;
#127005=CARTESIAN_POINT ( 'NONE',  ( -57.48921356237308800, -27.52281430457095368, 5.000000000000000000 ) ) ;
#127007=DIRECTION ( 'NONE',  ( 0.000000000000000000, 1.000000000000000000, 0.000000000000000000 ) ) ;
#127008=ORIENTED_EDGE ( 'NONE', *, *, #16168, .F. ) ;
#127009=ORIENTED_EDGE ( 'NONE', *, *, #45403, .F. ) ;
#127010=DIRECTION ( 'NONE',  ( 0.6830127018922180770, -0.6830127018922204085, -0.2588190451025213501 ) ) ;
#127011=ORIENTED_EDGE ( 'NONE', *, *, #124002, .F. ) ;
#127012=VECTOR ( 'NONE', #84177, 1000.000000000000227 ) ;
#127013=PLANE ( 'NONE',  #4776 ) ;
#127015=ORIENTED_EDGE ( 'NONE', *, *, #132572, .F. ) ;
#127017=AXIS2_PLACEMENT_3D ( 'NONE', #107236, #132609, #30405 ) ;
#127018=VECTOR ( 'NONE', #46195, 1000.000000000000000 ) ;
#127019=VECTOR ( 'NONE', #127577, 1000.000000000000000 ) ;
#127020=LINE ( 'NONE', #37912, #118346 ) ;
#127021=AXIS2_PLACEMENT_3D ( 'NONE', #49341, #126160, #24685 ) ;
#127022=EDGE_CURVE ( 'NONE', #9261, #88406, #67524, .T. ) ;
#127023=FACE_BOUND ( 'NONE', #105202, .T. ) ;
#127024=CARTESIAN_POINT ( 'NONE',  ( 24.81246187583929697, -22.22500000000000142, 4.000000000000000000 ) ) ;
#127025=CARTESIAN_POINT ( 'NONE',  ( 66.48921356237309510, -27.52281430457101763, 5.000000000000000000 ) ) ;
#127026=DIRECTION ( 'NONE',  ( -0.7071067811865486830, 0.7071067811865464625, 0.000000000000000000 ) ) ;
#127028=PLANE ( 'NONE',  #112866 ) ;
#127029=CARTESIAN_POINT ( 'NONE',  ( -18.48921356237309510, -27.52281430457068367, 5.000000000000000000 ) ) ;
#127030=VERTEX_POINT ( 'NONE', #56670 ) ;
#127031=ORIENTED_EDGE ( 'NONE', *, *, #13063, .F. ) ;
#127032=VECTOR ( 'NONE', #95508, 1000.000000000000000 ) ;
#127033=VECTOR ( 'NONE', #14060, 999.9999999999998863 ) ;
#127034=CARTESIAN_POINT ( 'NONE',  ( -63.48921356237309510, -27.52281430457099631, 5.000000000000000000 ) ) ;
#127035=VERTEX_POINT ( 'NONE', #34162 ) ;
#127036=EDGE_LOOP ( 'NONE', ( #114259, #17226, #88193, #137790 ) ) ;
#127038=ORIENTED_EDGE ( 'NONE', *, *, #139230, .F. ) ;
#127039=CARTESIAN_POINT ( 'NONE',  ( -24.18398860626899705, 28.73617430169804265, 5.000000000000000000 ) ) ;
#127041=EDGE_LOOP ( 'NONE', ( #28511, #64024, #52696, #13249 ) ) ;
#127042=LINE ( 'NONE', #114731, #116207 ) ;
#127043=VECTOR ( 'NONE', #102890, 1000.000000000000000 ) ;
#127044=VECTOR ( 'NONE', #36754, 999.9999999999998863 ) ;
#127048=EDGE_CURVE ( 'NONE', #90674, #87848, #58820, .T. ) ;
#127049=DIRECTION ( 'NONE',  ( -0.7071067811865486830, -0.7071067811865464625, 0.000000000000000000 ) ) ;
#127050=CARTESIAN_POINT ( 'NONE',  ( -6.707106781186489286, -6.740707523384216415, 5.000000000000000000 ) ) ;
#127051=CARTESIAN_POINT ( 'NONE',  ( 0.000000000000000000, 0.000000000000000000, 5.000000000000000000 ) ) ;
#127053=CARTESIAN_POINT ( 'NONE',  ( 29.99999999999979394, -9.412538124160654718, 4.000000000000000000 ) ) ;
#127054=ORIENTED_EDGE ( 'NONE', *, *, #23334, .T. ) ;
#127055=VECTOR ( 'NONE', #105886, 1000.000000000000227 ) ;
#127056=ORIENTED_EDGE ( 'NONE', *, *, #22006, .F. ) ;
#127057=VECTOR ( 'NONE', #80655, 1000.000000000000000 ) ;
#127059=( BOUNDED_CURVE ( )  B_SPLINE_CURVE ( 3, ( #84932, #85629, #129145, #76204 ),
 .UNSPECIFIED., .F., .T. ) 
 B_SPLINE_CURVE_WITH_KNOTS ( ( 4, 4 ),
 ( 5.005968288816728062, 5.074607125596327428 ),
 .UNSPECIFIED. ) 
 CURVE ( )  GEOMETRIC_REPRESENTATION_ITEM ( )  RATIONAL_B_SPLINE_CURVE ( ( 1.000000000000000000, 0.9996074310407765395, 0.9996074310407765395, 1.000000000000000000 ) ) 
 REPRESENTATION_ITEM ( '' )  );
#127060=LINE ( 'NONE', #36497, #69835 ) ;
#127061=VERTEX_POINT ( 'NONE', #3619 ) ;
#127062=VECTOR ( 'NONE', #25854, 1000.000000000000000 ) ;
#127063=ORIENTED_EDGE ( 'NONE', *, *, #9915, .T. ) ;
#127066=DIRECTION ( 'NONE',  ( -0.7071067811865486830, 0.7071067811865464625, 0.000000000000000000 ) ) ;
#127068=FACE_OUTER_BOUND ( 'NONE', #96322, .T. ) ;
#127070=VECTOR ( 'NONE', #88466, 1000.000000000000000 ) ;
#127071=LINE ( 'NONE', #116206, #76416 ) ;
#127073=DIRECTION ( 'NONE',  ( 0.7071067811865487940, 0.7071067811865463515, 0.000000000000000000 ) ) ;
#127075=FACE_OUTER_BOUND ( 'NONE', #112436, .T. ) ;
#127077=DIRECTION ( 'NONE',  ( -0.7071067811865487940, 0.7071067811865463515, 0.000000000000000000 ) ) ;
#127079=VECTOR ( 'NONE', #93218, 999.9999999999998863 ) ;
#127080=FACE_OUTER_BOUND ( 'NONE', #136369, .T. ) ;
#127081=ORIENTED_EDGE ( 'NONE', *, *, #118790, .T. ) ;
#127082=LINE ( 'NONE', #72039, #51703 ) ;
#127083=EDGE_LOOP ( 'NONE', ( #18621, #46090, #44842, #88820 ) ) ;
#127084=CARTESIAN_POINT ( 'NONE',  ( 7.499999999999951150, -12.08601207473287964, -10.46905243149095988 ) ) ;
#127085=DIRECTION ( 'NONE',  ( -0.7071067811865486830, -0.7071067811865464625, -0.000000000000000000 ) ) ;
#127086=DIRECTION ( 'NONE',  ( -0.6830127018922180770, -0.6830127018922204085, -0.2588190451025213501 ) ) ;
#127088=LINE ( 'NONE', #72050, #91217 ) ;
#127090=CARTESIAN_POINT ( 'NONE',  ( -34.42500000000001137, 0.000000000000000000, 4.500000000000000888 ) ) ;
#127091=ORIENTED_EDGE ( 'NONE', *, *, #123840, .T. ) ;
#127092=DIRECTION ( 'NONE',  ( 0.7071067811865487940, 0.7071067811865463515, 0.000000000000000000 ) ) ;
#127093=CARTESIAN_POINT ( 'NONE',  ( -27.18398860626900060, 28.73617430169806042, 5.000000000000000000 ) ) ;
#127094=DIRECTION ( 'NONE',  ( 0.7071067811865487940, 0.7071067811865463515, 0.000000000000000000 ) ) ;
#127097=ORIENTED_EDGE ( 'NONE', *, *, #39241, .F. ) ;
#127098=ORIENTED_EDGE ( 'NONE', *, *, #27301, .F. ) ;
#127099=CARTESIAN_POINT ( 'NONE',  ( 33.18398860626899705, 28.73617430169810305, 5.000000000000000000 ) ) ;
#127100=CARTESIAN_POINT ( 'NONE',  ( 12.18398860626900060, 28.73617430169795739, 5.000000000000000000 ) ) ;
#127103=EDGE_CURVE ( 'NONE', #14082, #7225, #31018, .T. ) ;
#127104=CARTESIAN_POINT ( 'NONE',  ( -30.29974487139158867, -27.71228299555227537, 4.000000000000000000 ) ) ;
#127105=CARTESIAN_POINT ( 'NONE',  ( 0.000000000000000000, 0.000000000000000000, 5.000000000000000000 ) ) ;
#127107=ADVANCED_FACE ( 'NONE', ( #131750 ), #19402, .F. ) ;
#127108=ORIENTED_EDGE ( 'NONE', *, *, #88725, .F. ) ;
#127110=EDGE_CURVE ( 'NONE', #18669, #94043, #63654, .T. ) ;
#127111=FACE_OUTER_BOUND ( 'NONE', #128672, .T. ) ;
#127112=CARTESIAN_POINT ( 'NONE',  ( 32.99999999999976552, 10.93112307739207623, 4.000000000000000000 ) ) ;
#127115=PLANE ( 'NONE',  #88171 ) ;
#127116=EDGE_LOOP ( 'NONE', ( #6517, #135262, #75494, #70199 ) ) ;
#127118=VERTEX_POINT ( 'NONE', #131033 ) ;
#127119=EDGE_CURVE ( 'NONE', #42800, #122052, #99820, .T. ) ;
#127120=ORIENTED_EDGE ( 'NONE', *, *, #70732, .F. ) ;
#127121=DIRECTION ( 'NONE',  ( -0.000000000000000000, -0.3543493200069152693, 0.9351131265310292928 ) ) ;
#127122=AXIS2_PLACEMENT_3D ( 'NONE', #72186, #83023, #14892 ) ;
#127123=VECTOR ( 'NONE', #102983, 1000.000000000000000 ) ;
#127125=DIRECTION ( 'NONE',  ( 0.7071067811865486830, -0.7071067811865464625, -0.000000000000000000 ) ) ;
#127126=CARTESIAN_POINT ( 'NONE',  ( 0.000000000000000000, 0.000000000000000000, 5.000000000000000000 ) ) ;
#127127=VECTOR ( 'NONE', #3969, 1000.000000000000000 ) ;
#127128=ADVANCED_FACE ( 'NONE', ( #110661 ), #485, .F. ) ;
#127129=LINE ( 'NONE', #135879, #9276 ) ;
#127130=ADVANCED_FACE ( 'NONE', ( #33182 ), #119402, .F. ) ;
#127131=CARTESIAN_POINT ( 'NONE',  ( 54.48921356237310221, -27.52281430457093236, 5.000000000000000000 ) ) ;
#127132=PLANE ( 'NONE',  #110152 ) ;
#127133=ORIENTED_EDGE ( 'NONE', *, *, #142233, .T. ) ;
#127134=LINE ( 'NONE', #27109, #25538 ) ;
#127135=CARTESIAN_POINT ( 'NONE',  ( -14.70025512860841133, -27.71228299555195917, 4.000000000000000000 ) ) ;
#127138=DIRECTION ( 'NONE',  ( -0.3543493200069162685, -0.000000000000000000, -0.9351131265310288487 ) ) ;
#127139=LINE ( 'NONE', #91664, #65914 ) ;
#127140=EDGE_CURVE ( 'NONE', #142129, #131532, #42620, .T. ) ;
#127143=CARTESIAN_POINT ( 'NONE',  ( 4.031635159221891307, 2.259292476615694323, 13.77329220150638456 ) ) ;
#127145=ORIENTED_EDGE ( 'NONE', *, *, #19558, .F. ) ;
#127147=LINE ( 'NONE', #85078, #30864 ) ;
#127148=LINE ( 'NONE', #105396, #97123 ) ;
#127151=ORIENTED_EDGE ( 'NONE', *, *, #111181, .F. ) ;
#127153=VECTOR ( 'NONE', #142335, 999.9999999999998863 ) ;
#127154=LINE ( 'NONE', #105401, #132429 ) ;
#127156=EDGE_CURVE ( 'NONE', #115946, #68778, #109267, .T. ) ;
#127157=FACE_OUTER_BOUND ( 'NONE', #123181, .T. ) ;
#127158=VERTEX_POINT ( 'NONE', #21553 ) ;
#127159=ORIENTED_EDGE ( 'NONE', *, *, #50186, .T. ) ;
#127160=CARTESIAN_POINT ( 'NONE',  ( -2.999999999999976463, -0.03360074219773551141, 5.000000000000000000 ) ) ;
#127163=DIRECTION ( 'NONE',  ( -0.000000000000000000, 0.3543493200069153248, 0.9351131265310292928 ) ) ;
#127164=FACE_OUTER_BOUND ( 'NONE', #121468, .T. ) ;
#127165=VECTOR ( 'NONE', #14453, 1000.000000000000000 ) ;
#127166=DIRECTION ( 'NONE',  ( -0.6830127018922181881, 0.6830127018922202975, -0.2588190451025214056 ) ) ;
#127167=CARTESIAN_POINT ( 'NONE',  ( -8.903329358125901649, -2.240707523384260824, 15.26439735382750484 ) ) ;
#127168=DIRECTION ( 'NONE',  ( 0.7071067811865486830, -0.7071067811865464625, -0.000000000000000000 ) ) ;
#127169=ORIENTED_EDGE ( 'NONE', *, *, #128575, .F. ) ;
#127170=DIRECTION ( 'NONE',  ( -0.7071067811865486830, -0.7071067811865464625, 0.000000000000000000 ) ) ;
#127171=CARTESIAN_POINT ( 'NONE',  ( 1.040834085586084257E-14, 11.58746187583913034, 4.000000000000000000 ) ) ;
#127172=CARTESIAN_POINT ( 'NONE',  ( -24.79333936457829779, 21.75929247661549581, 4.998822639870701856 ) ) ;
#127173=VECTOR ( 'NONE', #80285, 1000.000000000000000 ) ;
#127174=DIRECTION ( 'NONE',  ( 0.6830127018922180770, -0.6830127018922204085, -0.2588190451025213501 ) ) ;
#127175=VECTOR ( 'NONE', #55449, 999.9999999999998863 ) ;
#127176=EDGE_CURVE ( 'NONE', #16650, #27906, #65815, .T. ) ;
#127177=VERTEX_POINT ( 'NONE', #143321 ) ;
#127178=ORIENTED_EDGE ( 'NONE', *, *, #68491, .T. ) ;
#127179=PLANE ( 'NONE',  #1367 ) ;
#127180=CARTESIAN_POINT ( 'NONE',  ( 21.48921356237309155, -27.52281430457070499, 5.000000000000000000 ) ) ;
#127182=ADVANCED_FACE ( 'NONE', ( #44026 ), #88243, .F. ) ;
#127183=DIRECTION ( 'NONE',  ( -0.7071067811865486830, -0.7071067811865464625, 0.000000000000000000 ) ) ;
#127184=CARTESIAN_POINT ( 'NONE',  ( -29.99999999999979039, -0.8619312979532244290, -5.102805207349895511 ) ) ;
#127185=EDGE_LOOP ( 'NONE', ( #127954, #48878, #22354, #75645 ) ) ;
#127186=ORIENTED_EDGE ( 'NONE', *, *, #2329, .F. ) ;
#127188=DIRECTION ( 'NONE',  ( -0.7071067811865486830, -0.7071067811865464625, 0.000000000000000000 ) ) ;
#127190=VERTEX_POINT ( 'NONE', #114264 ) ;
#127191=ORIENTED_EDGE ( 'NONE', *, *, #89221, .T. ) ;
#127192=ADVANCED_FACE ( 'NONE', ( #57779 ), #78797, .T. ) ;
#127193=DIRECTION ( 'NONE',  ( 1.000000000000000000, 0.000000000000000000, 0.000000000000000000 ) ) ;
#127194=ORIENTED_EDGE ( 'NONE', *, *, #86110, .T. ) ;
#127195=PLANE ( 'NONE',  #10913 ) ;
#127196=CARTESIAN_POINT ( 'NONE',  ( -69.18398860626899705, 28.73617430169835529, 5.000000000000000000 ) ) ;
#127197=EDGE_CURVE ( 'NONE', #13173, #108474, #100397, .T. ) ;
#127198=FACE_BOUND ( 'NONE', #43485, .T. ) ;
#127199=FACE_OUTER_BOUND ( 'NONE', #139353, .T. ) ;
#127202=CARTESIAN_POINT ( 'NONE',  ( 54.18398860626899705, 28.73617430169825226, 5.000000000000000000 ) ) ;
#127203=VERTEX_POINT ( 'NONE', #14236 ) ;
#127204=DIRECTION ( 'NONE',  ( -0.3543493200069162685, -0.000000000000000000, -0.9351131265310288487 ) ) ;
#127206=ORIENTED_EDGE ( 'NONE', *, *, #105908, .F. ) ;
#127207=ORIENTED_EDGE ( 'NONE', *, *, #116017, .T. ) ;
#127209=ORIENTED_EDGE ( 'NONE', *, *, #21178, .F. ) ;
#127210=CARTESIAN_POINT ( 'NONE',  ( -42.18398860626899705, 28.73617430169816700, 5.000000000000000000 ) ) ;
#127211=DIRECTION ( 'NONE',  ( -0.7071067811865486830, -0.7071067811865464625, 0.000000000000000000 ) ) ;
#127213=EDGE_LOOP ( 'NONE', ( #57892, #29866, #22481, #83265 ) ) ;
#127214=CARTESIAN_POINT ( 'NONE',  ( 20.99999999999985789, -11.35517001088070010, -1.126524801160061262 ) ) ;
#127215=EDGE_CURVE ( 'NONE', #108894, #116464, #1195, .T. ) ;
#127217=CARTESIAN_POINT ( 'NONE',  ( 21.72281430457044493, -21.72500000000000142, 5.000000000000000000 ) ) ;
#127218=PLANE ( 'NONE',  #137651 ) ;
#127219=PLANE ( 'NONE',  #6844 ) ;
#127220=AXIS2_PLACEMENT_3D ( 'NONE', #77872, #22728, #59703 ) ;
#127223=VECTOR ( 'NONE', #71766, 1000.000000000000000 ) ;
#127224=ORIENTED_EDGE ( 'NONE', *, *, #24460, .F. ) ;
#127225=DIRECTION ( 'NONE',  ( 0.7071067811865487940, 0.7071067811865463515, 0.000000000000000000 ) ) ;
#127226=LINE ( 'NONE', #91749, #76650 ) ;
#127227=VECTOR ( 'NONE', #120801, 1000.000000000000000 ) ;
#127231=EDGE_CURVE ( 'NONE', #76404, #24129, #36019, .T. ) ;
#127232=ORIENTED_EDGE ( 'NONE', *, *, #5869, .T. ) ;
#127234=ORIENTED_EDGE ( 'NONE', *, *, #44018, .T. ) ;
#127235=AXIS2_PLACEMENT_3D ( 'NONE', #67430, #134837, #12297 ) ;
#127237=VECTOR ( 'NONE', #8831, 1000.000000000000000 ) ;
#127240=ORIENTED_EDGE ( 'NONE', *, *, #108431, .F. ) ;
#127241=CARTESIAN_POINT ( 'NONE',  ( 3.707106781186525257, 5.259292476615661016, 5.000000000000000000 ) ) ;
#127242=EDGE_LOOP ( 'NONE', ( #126537, #70656, #103767, #49239 ) ) ;
#127243=CARTESIAN_POINT ( 'NONE',  ( 18.79333936457835108, 21.75929247661549937, 4.998822639870708073 ) ) ;
#127245=AXIS2_PLACEMENT_3D ( 'NONE', #97987, #40761, #96516 ) ;
#127246=DIRECTION ( 'NONE',  ( 0.6830127018922181881, 0.6830127018922202975, -0.2588190451025214056 ) ) ;
#127247=DIRECTION ( 'NONE',  ( 0.7071067811865487940, -0.7071067811865463515, 0.000000000000000000 ) ) ;
#127249=EDGE_LOOP ( 'NONE', ( #121440, #95046, #82260, #78027 ) ) ;
#127250=ADVANCED_FACE ( 'NONE', ( #4015 ), #36696, .F. ) ;
#127251=DIRECTION ( 'NONE',  ( -0.7071067811865486830, -0.7071067811865464625, 0.000000000000000000 ) ) ;
#127252=LINE ( 'NONE', #72934, #6786 ) ;
#127253=ORIENTED_EDGE ( 'NONE', *, *, #9440, .F. ) ;
#127254=AXIS2_PLACEMENT_3D ( 'NONE', #123806, #59278, #114327 ) ;
#127256=VERTEX_POINT ( 'NONE', #100548 ) ;
#127257=EDGE_LOOP ( 'NONE', ( #65982, #45612, #72958, #38492 ) ) ;
#127258=VERTEX_POINT ( 'NONE', #3339 ) ;
#127259=EDGE_LOOP ( 'NONE', ( #134046, #18229, #73184, #133015 ) ) ;
#127260=FACE_OUTER_BOUND ( 'NONE', #31368, .T. ) ;
#127261=VECTOR ( 'NONE', #135077, 1000.000000000000227 ) ;
#127263=DIRECTION ( 'NONE',  ( 0.000000000000000000, 0.000000000000000000, -1.000000000000000000 ) ) ;
#127264=VECTOR ( 'NONE', #132534, 1000.000000000000000 ) ;
#127265=CARTESIAN_POINT ( 'NONE',  ( -8.999999999999934275, 7.552185695429090906, 5.000000000000000000 ) ) ;
#127266=CARTESIAN_POINT ( 'NONE',  ( 25.49999999999982592, 16.77039438581781639, 0.4657186855307159368 ) ) ;
#127267=ORIENTED_EDGE ( 'NONE', *, *, #45906, .F. ) ;
#127268=AXIS2_PLACEMENT_3D ( 'NONE', #104261, #115125, #139805 ) ;
#127270=VERTEX_POINT ( 'NONE', #47625 ) ;
#127271=VECTOR ( 'NONE', #46064, 1000.000000000000227 ) ;
#127272=PLANE ( 'NONE',  #26291 ) ;
#127274=LINE ( 'NONE', #71487, #57836 ) ;
#127275=EDGE_CURVE ( 'NONE', #65672, #88912, #2631, .T. ) ;
#127276=CARTESIAN_POINT ( 'NONE',  ( 25.74845587132409364, -11.24070752338416490, 10.39518518046003415 ) ) ;
#127277=DIRECTION ( 'NONE',  ( -0.000000000000000000, -0.3543493200069152693, 0.9351131265310292928 ) ) ;
#127278=EDGE_LOOP ( 'NONE', ( #116672, #44195, #25936, #15021, #69695, #88074 ) ) ;
#127279=EDGE_CURVE ( 'NONE', #80487, #29533, #14938, .T. ) ;
#127280=VERTEX_POINT ( 'NONE', #123011 ) ;
#127281=ORIENTED_EDGE ( 'NONE', *, *, #137379, .T. ) ;
#127283=PLANE ( 'NONE',  #51092 ) ;
#127285=VECTOR ( 'NONE', #91322, 1000.000000000000000 ) ;
#127286=DIRECTION ( 'NONE',  ( 0.6830127018922181881, 0.6830127018922202975, -0.2588190451025214056 ) ) ;
#127287=CARTESIAN_POINT ( 'NONE',  ( 34.92499999999998295, -14.14387692260744878, 4.000000000000000000 ) ) ;
#127293=CARTESIAN_POINT ( 'NONE',  ( 34.49999999999976552, 4.087461875839198733, 4.000000000000000000 ) ) ;
#127294=CARTESIAN_POINT ( 'NONE',  ( -5.721745484314237906, 8.259292476615630818, 11.78515199841149297 ) ) ;
#127295=LINE ( 'NONE', #108360, #74477 ) ;
#127296=DIRECTION ( 'NONE',  ( 0.6830127018922181881, 0.6830127018922202975, -0.2588190451025214056 ) ) ;
#127297=ORIENTED_EDGE ( 'NONE', *, *, #92520, .F. ) ;
#127298=VECTOR ( 'NONE', #80051, 1000.000000000000227 ) ;
#127299=LINE ( 'NONE', #137484, #59228 ) ;
#127300=EDGE_LOOP ( 'NONE', ( #132365, #73597, #104439, #108992 ) ) ;
#127301=LINE ( 'NONE', #28005, #59931 ) ;
#127302=DIRECTION ( 'NONE',  ( -0.7071067811865487940, 0.7071067811865463515, -0.000000000000000000 ) ) ;
#127304=EDGE_CURVE ( 'NONE', #60449, #17946, #91115, .T. ) ;
#127306=DIRECTION ( 'NONE',  ( -0.7071067811865487940, 0.7071067811865463515, -0.000000000000000000 ) ) ;
#127307=FACE_OUTER_BOUND ( 'NONE', #20900, .T. ) ;
#127308=ORIENTED_EDGE ( 'NONE', *, *, #93860, .F. ) ;
#127309=VERTEX_POINT ( 'NONE', #111396 ) ;
#127310=DIRECTION ( 'NONE',  ( -0.6830127018922181881, 0.6830127018922202975, -0.2588190451025214056 ) ) ;
#127312=ORIENTED_EDGE ( 'NONE', *, *, #75388, .T. ) ;
#127313=DIRECTION ( 'NONE',  ( 0.7071067811865487940, 0.7071067811865463515, -0.000000000000000000 ) ) ;
#127314=EDGE_CURVE ( 'NONE', #39875, #132680, #12084, .T. ) ;
#127318=ORIENTED_EDGE ( 'NONE', *, *, #95893, .T. ) ;
#127319=LINE ( 'NONE', #114305, #58530 ) ;
#127320=FACE_OUTER_BOUND ( 'NONE', #125765, .T. ) ;
#127322=CARTESIAN_POINT ( 'NONE',  ( -63.29974487139158867, -27.71228299555250274, 4.000000000000000000 ) ) ;
#127324=CARTESIAN_POINT ( 'NONE',  ( -33.29974487139158867, -27.71228299555229313, 4.000000000000000000 ) ) ;
#127325=ORIENTED_EDGE ( 'NONE', *, *, #105243, .F. ) ;
#127327=ORIENTED_EDGE ( 'NONE', *, *, #80829, .T. ) ;
#127330=DIRECTION ( 'NONE',  ( 1.000000000000000000, 0.000000000000000000, 0.000000000000000000 ) ) ;
#127331=VECTOR ( 'NONE', #30003, 999.9999999999998863 ) ;
#127332=EDGE_CURVE ( 'NONE', #101826, #11525, #34576, .T. ) ;
#127333=CARTESIAN_POINT ( 'NONE',  ( -23.99451991528749062, 28.92564299267954908, 4.000000000000000000 ) ) ;
#127334=DIRECTION ( 'NONE',  ( -0.6830127018922180770, -0.6830127018922204085, -0.2588190451025213501 ) ) ;
#127336=VECTOR ( 'NONE', #85515, 999.9999999999998863 ) ;
#127337=VECTOR ( 'NONE', #32084, 1000.000000000000114 ) ;
#127338=VECTOR ( 'NONE', #78269, 1000.000000000000000 ) ;
#127339=DIRECTION ( 'NONE',  ( 0.7071067811865486830, -0.7071067811865464625, -0.000000000000000000 ) ) ;
#127340=VECTOR ( 'NONE', #50404, 1000.000000000000000 ) ;
#127342=DIRECTION ( 'NONE',  ( 0.7071067811865487940, -0.7071067811865463515, 0.000000000000000000 ) ) ;
#127344=FACE_OUTER_BOUND ( 'NONE', #27568, .T. ) ;
#127345=ORIENTED_EDGE ( 'NONE', *, *, #71039, .F. ) ;
#127346=EDGE_CURVE ( 'NONE', #111310, #61200, #24399, .T. ) ;
#127347=DIRECTION ( 'NONE',  ( 0.7071067811865486830, -0.7071067811865464625, -0.000000000000000000 ) ) ;
#127348=CARTESIAN_POINT ( 'NONE',  ( -34.75611968250420603, 13.70565069852392703, 4.955485411084897152 ) ) ;
#127350=VECTOR ( 'NONE', #35351, 1000.000000000000000 ) ;
#127352=VERTEX_POINT ( 'NONE', #15614 ) ;
#127353=EDGE_CURVE ( 'NONE', #18088, #107805, #139374, .T. ) ;
#127354=ORIENTED_EDGE ( 'NONE', *, *, #112592, .F. ) ;
#127356=ORIENTED_EDGE ( 'NONE', *, *, #95013, .T. ) ;
#127357=DIRECTION ( 'NONE',  ( -0.7071067811865486830, -0.7071067811865464625, -0.000000000000000000 ) ) ;
#127359=DIRECTION ( 'NONE',  ( -0.3543493200069162685, -0.000000000000000000, -0.9351131265310288487 ) ) ;
#127360=PLANE ( 'NONE',  #94023 ) ;
#127361=ORIENTED_EDGE ( 'NONE', *, *, #128762, .F. ) ;
#127362=DIRECTION ( 'NONE',  ( -0.000000000000000000, 0.000000000000000000, 1.000000000000000000 ) ) ;
#127365=VERTEX_POINT ( 'NONE', #16347 ) ;
#127366=EDGE_CURVE ( 'NONE', #12589, #96735, #93934, .T. ) ;
#127367=CARTESIAN_POINT ( 'NONE',  ( 68.99451991528748351, 28.92564299267986172, 4.000000000000000000 ) ) ;
#127368=DIRECTION ( 'NONE',  ( 0.7071067811865487940, 0.7071067811865463515, 0.000000000000000000 ) ) ;
#127369=LINE ( 'NONE', #28068, #23818 ) ;
#127371=VERTEX_POINT ( 'NONE', #117799 ) ;
#127372=ORIENTED_EDGE ( 'NONE', *, *, #36818, .F. ) ;
#127375=CARTESIAN_POINT ( 'NONE',  ( 29.99999999999979039, -12.03360074219761700, 5.000000000000000000 ) ) ;
#127376=FACE_OUTER_BOUND ( 'NONE', #34992, .T. ) ;
#127378=CARTESIAN_POINT ( 'NONE',  ( -2.475998614145493715, 22.03583458319438293, 4.979811245910087614 ) ) ;
#127379=LINE ( 'NONE', #61460, #1679 ) ;
#127380=CARTESIAN_POINT ( 'NONE',  ( -38.99451991528749062, 28.92564299267965211, 4.000000000000000000 ) ) ;
#127381=ORIENTED_EDGE ( 'NONE', *, *, #131504, .F. ) ;
#127382=VECTOR ( 'NONE', #127204, 1000.000000000000227 ) ;
#127383=ORIENTED_EDGE ( 'NONE', *, *, #11952, .T. ) ;
#127386=EDGE_LOOP ( 'NONE', ( #101950, #102958, #75308 ) ) ;
#127387=VECTOR ( 'NONE', #31407, 1000.000000000000227 ) ;
#127388=LINE ( 'NONE', #26657, #82544 ) ;
#127389=ORIENTED_EDGE ( 'NONE', *, *, #97999, .F. ) ;
#127391=DIRECTION ( 'NONE',  ( 0.7071067811865487940, 0.7071067811865463515, 0.000000000000000000 ) ) ;
#127392=EDGE_CURVE ( 'NONE', #58699, #121778, #129600, .T. ) ;
#127393=DIRECTION ( 'NONE',  ( 0.7071067811865487940, 0.7071067811865463515, 0.000000000000000000 ) ) ;
#127394=DIRECTION ( 'NONE',  ( 0.3543493200069162685, -0.000000000000000000, -0.9351131265310288487 ) ) ;
#127395=VECTOR ( 'NONE', #112994, 1000.000000000000000 ) ;
#127396=LINE ( 'NONE', #95480, #14354 ) ;
#127397=ORIENTED_EDGE ( 'NONE', *, *, #61486, .T. ) ;
#127398=DIRECTION ( 'NONE',  ( 0.7071067811865486830, -0.7071067811865464625, -0.000000000000000000 ) ) ;
#127399=DIRECTION ( 'NONE',  ( 0.7071067811865487940, -0.7071067811865463515, 0.000000000000000000 ) ) ;
#127400=VERTEX_POINT ( 'NONE', #83821 ) ;
#127401=EDGE_CURVE ( 'NONE', #3555, #103699, #84519, .T. ) ;
#127402=CARTESIAN_POINT ( 'NONE',  ( -10.82816939922344979, -11.24070752338417023, 4.000000000000000000 ) ) ;
#127403=VERTEX_POINT ( 'NONE', #128712 ) ;
#127404=VERTEX_POINT ( 'NONE', #38853 ) ;
#127406=EDGE_CURVE ( 'NONE', #80026, #49145, #126551, .T. ) ;
#127407=ORIENTED_EDGE ( 'NONE', *, *, #56085, .F. ) ;
#127410=VECTOR ( 'NONE', #81703, 1000.000000000000000 ) ;
#127411=VERTEX_POINT ( 'NONE', #61368 ) ;
#127412=AXIS2_PLACEMENT_3D ( 'NONE', #114600, #61008, #48659 ) ;
#127413=FACE_OUTER_BOUND ( 'NONE', #71826, .T. ) ;
#127414=DIRECTION ( 'NONE',  ( 0.7071067811865487940, 0.7071067811865463515, -0.000000000000000000 ) ) ;
#127416=CARTESIAN_POINT ( 'NONE',  ( 34.92499999999998295, -15.89852273831277074, -9.446427897663607354 ) ) ;
#127417=EDGE_CURVE ( 'NONE', #92047, #91018, #29388, .T. ) ;
#127418=DIRECTION ( 'NONE',  ( -0.7071067811865486830, -0.7071067811865464625, 0.000000000000000000 ) ) ;
#127419=PLANE ( 'NONE',  #41773 ) ;
#127420=CARTESIAN_POINT ( 'NONE',  ( 60.48921356237309510, -27.52281430457097500, 5.000000000000000000 ) ) ;
#127422=CARTESIAN_POINT ( 'NONE',  ( 28.82816939922332722, 15.75929247661554733, 4.000000000000000000 ) ) ;
#127423=EDGE_CURVE ( 'NONE', #62049, #11462, #17102, .T. ) ;
#127424=CARTESIAN_POINT ( 'NONE',  ( 7.499999999999947597, -19.91253812416055169, 4.000000000000000000 ) ) ;
#127425=VECTOR ( 'NONE', #122397, 1000.000000000000000 ) ;
#127426=CARTESIAN_POINT ( 'NONE',  ( -44.99451991528749772, 28.92564299267969474, 4.000000000000000000 ) ) ;
#127427=VECTOR ( 'NONE', #5919, 1000.000000000000000 ) ;
#127430=VERTEX_POINT ( 'NONE', #83076 ) ;
#127431=ORIENTED_EDGE ( 'NONE', *, *, #123066, .T. ) ;
#127433=VECTOR ( 'NONE', #89813, 1000.000000000000000 ) ;
#127435=VECTOR ( 'NONE', #10664, 1000.000000000000000 ) ;
#127436=ORIENTED_EDGE ( 'NONE', *, *, #9171, .T. ) ;
#127437=VECTOR ( 'NONE', #114439, 1000.000000000000227 ) ;
#127438=VECTOR ( 'NONE', #46284, 1000.000000000000000 ) ;
#127439=VECTOR ( 'NONE', #75221, 1000.000000000000227 ) ;
#127440=FACE_OUTER_BOUND ( 'NONE', #52140, .T. ) ;
#127441=DIRECTION ( 'NONE',  ( 0.7071067811865486830, -0.7071067811865464625, -0.000000000000000000 ) ) ;
#127443=DIRECTION ( 'NONE',  ( 0.3543493200069164351, 2.781805975412904658E-17, -0.9351131265310288487 ) ) ;
#127444=EDGE_LOOP ( 'NONE', ( #90289, #5077, #30879, #122993 ) ) ;
#127445=VECTOR ( 'NONE', #71733, 1000.000000000000000 ) ;
#127446=VERTEX_POINT ( 'NONE', #116415 ) ;
#127448=PLANE ( 'NONE',  #130347 ) ;
#127449=LINE ( 'NONE', #94097, #36682 ) ;
#127451=ORIENTED_EDGE ( 'NONE', *, *, #131545, .T. ) ;
#127452=EDGE_CURVE ( 'NONE', #35648, #110736, #127274, .T. ) ;
#127453=ORIENTED_EDGE ( 'NONE', *, *, #97162, .T. ) ;
#127454=EDGE_LOOP ( 'NONE', ( #7446, #105859, #120030, #96715 ) ) ;
#127457=CARTESIAN_POINT ( 'NONE',  ( 16.17183060077636370, -5.240707523384223521, 4.000000000000000000 ) ) ;
#127458=CARTESIAN_POINT ( 'NONE',  ( -9.707106781186475075, -3.740707523384241728, 5.000000000000000000 ) ) ;
#127459=DIRECTION ( 'NONE',  ( 0.6830127018922181881, 0.6830127018922202975, -0.2588190451025214056 ) ) ;
#127460=PLANE ( 'NONE',  #18136 ) ;
#127461=ADVANCED_FACE ( 'NONE', ( #49758 ), #27976, .T. ) ;
#127462=ADVANCED_FACE ( 'NONE', ( #6175 ), #27240, .F. ) ;
#127464=VECTOR ( 'NONE', #118984, 1000.000000000000000 ) ;
#127465=DIRECTION ( 'NONE',  ( 0.6830127018922181881, 0.6830127018922202975, -0.2588190451025214056 ) ) ;
#127466=PLANE ( 'NONE',  #97519 ) ;
#127467=CARTESIAN_POINT ( 'NONE',  ( -0.4892135623730947680, -27.52281430457055578, 5.000000000000000000 ) ) ;
#127468=AXIS2_PLACEMENT_3D ( 'NONE', #5162, #29096, #18177 ) ;
#127469=ORIENTED_EDGE ( 'NONE', *, *, #34613, .T. ) ;
#127470=LINE ( 'NONE', #48483, #39425 ) ;
#127472=AXIS2_PLACEMENT_3D ( 'NONE', #119954, #19256, #130898 ) ;
#127473=EDGE_CURVE ( 'NONE', #84275, #34917, #72246, .T. ) ;
#127474=ORIENTED_EDGE ( 'NONE', *, *, #61915, .T. ) ;
#127475=CARTESIAN_POINT ( 'NONE',  ( 21.48921356237309155, -27.52281430457070499, 5.000000000000000000 ) ) ;
#127476=FACE_OUTER_BOUND ( 'NONE', #28447, .T. ) ;
#127477=ORIENTED_EDGE ( 'NONE', *, *, #59265, .T. ) ;
#127478=ADVANCED_FACE ( 'NONE', ( #49032 ), #93227, .T. ) ;
#127480=EDGE_CURVE ( 'NONE', #66788, #6851, #40309, .T. ) ;
#127481=LINE ( 'NONE', #16558, #7463 ) ;
#127482=LINE ( 'NONE', #49944, #115527 ) ;
#127483=VERTEX_POINT ( 'NONE', #56736 ) ;
#127484=DIRECTION ( 'NONE',  ( -0.6830127018922181881, 0.6830127018922202975, -0.2588190451025214056 ) ) ;
#127486=ORIENTED_EDGE ( 'NONE', *, *, #40589, .T. ) ;
#127487=LINE ( 'NONE', #17292, #121544 ) ;
#127489=EDGE_CURVE ( 'NONE', #68456, #142084, #77042, .T. ) ;
#127490=FACE_OUTER_BOUND ( 'NONE', #91693, .T. ) ;
#127491=VECTOR ( 'NONE', #12648, 1000.000000000000000 ) ;
#127493=CARTESIAN_POINT ( 'NONE',  ( -32.20666063542130075, 21.75929247661549226, 4.998822639870715179 ) ) ;
#127494=DIRECTION ( 'NONE',  ( -0.7071067811865486830, 0.7071067811865464625, 0.000000000000000000 ) ) ;
#127495=CARTESIAN_POINT ( 'NONE',  ( -63.48921356237309510, -27.52281430457099631, 5.000000000000000000 ) ) ;
#127496=PLANE ( 'NONE',  #115444 ) ;
#127498=AXIS2_PLACEMENT_3D ( 'NONE', #22465, #130562, #21784 ) ;
#127500=DIRECTION ( 'NONE',  ( 0.7071067811865487940, 0.7071067811865463515, -0.000000000000000000 ) ) ;
#127502=LINE ( 'NONE', #60867, #76801 ) ;
#127503=LINE ( 'NONE', #61569, #1505 ) ;
#127504=ORIENTED_EDGE ( 'NONE', *, *, #102956, .F. ) ;
#127507=CARTESIAN_POINT ( 'NONE',  ( -25.17183060077628909, -20.24070752338406365, 4.000000000000000000 ) ) ;
#127508=ORIENTED_EDGE ( 'NONE', *, *, #46372, .T. ) ;
#127509=CARTESIAN_POINT ( 'NONE',  ( 47.99451991528749062, 28.92564299267971251, 4.000000000000000000 ) ) ;
#127510=LINE ( 'NONE', #113781, #113477 ) ;
#127511=ADVANCED_FACE ( 'NONE', ( #88622 ), #100203, .T. ) ;
#127514=ORIENTED_EDGE ( 'NONE', *, *, #141371, .T. ) ;
#127515=DIRECTION ( 'NONE',  ( -0.3543493200069162685, -0.000000000000000000, -0.9351131265310288487 ) ) ;
#127516=DIRECTION ( 'NONE',  ( 0.6830127018922180770, -0.6830127018922204085, -0.2588190451025213501 ) ) ;
#127517=PLANE ( 'NONE',  #62692 ) ;
#127518=LINE ( 'NONE', #7121, #79023 ) ;
#127519=CARTESIAN_POINT ( 'NONE',  ( 25.49999999999982947, 9.052185695429072254, 5.000000000000000000 ) ) ;
#127520=CARTESIAN_POINT ( 'NONE',  ( -24.20969143188526118, 6.176090689687629975, 5.000000000000000000 ) ) ;
#127521=EDGE_CURVE ( 'NONE', #88704, #16399, #121216, .T. ) ;
#127522=DIRECTION ( 'NONE',  ( -0.7071067811865486830, 0.7071067811865464625, 0.000000000000000000 ) ) ;
#127524=DIRECTION ( 'NONE',  ( -0.7071067811865486830, 0.7071067811865464625, 0.000000000000000000 ) ) ;
#127525=CARTESIAN_POINT ( 'NONE',  ( 15.32816939922343202, 8.259292476615637923, 4.000000000000000000 ) ) ;
#127526=DIRECTION ( 'NONE',  ( 1.000000000000000000, 0.000000000000000000, 0.000000000000000000 ) ) ;
#127528=EDGE_CURVE ( 'NONE', #46561, #58967, #33541, .T. ) ;
#127529=EDGE_LOOP ( 'NONE', ( #113592, #88583, #47047, #69260 ) ) ;
#127530=ORIENTED_EDGE ( 'NONE', *, *, #121688, .T. ) ;
#127532=ORIENTED_EDGE ( 'NONE', *, *, #24057, .T. ) ;
#127535=ORIENTED_EDGE ( 'NONE', *, *, #124819, .T. ) ;
#127538=LINE ( 'NONE', #118047, #62946 ) ;
#127539=CARTESIAN_POINT ( 'NONE',  ( -16.17183060077635659, -14.24070752338413648, 4.000000000000000000 ) ) ;
#127540=AXIS2_PLACEMENT_3D ( 'NONE', #137416, #47588, #105466 ) ;
#127541=VECTOR ( 'NONE', #86753, 1000.000000000000000 ) ;
#127543=ORIENTED_EDGE ( 'NONE', *, *, #8095, .F. ) ;
#127545=ORIENTED_EDGE ( 'NONE', *, *, #86219, .F. ) ;
#127547=AXIS2_PLACEMENT_3D ( 'NONE', #116933, #106028, #109624 ) ;
#127548=VECTOR ( 'NONE', #130737, 1000.000000000000000 ) ;
#127550=VECTOR ( 'NONE', #87370, 999.9999999999998863 ) ;
#127551=VECTOR ( 'NONE', #91881, 1000.000000000000000 ) ;
#127552=CARTESIAN_POINT ( 'NONE',  ( -5.999999999999951150, -6.412538124160692909, 4.000000000000000000 ) ) ;
#127553=CARTESIAN_POINT ( 'NONE',  ( 18.48921356237309510, -27.52281430457068367, 5.000000000000000000 ) ) ;
#127556=ORIENTED_EDGE ( 'NONE', *, *, #47915, .F. ) ;
#127557=ORIENTED_EDGE ( 'NONE', *, *, #33840, .T. ) ;
#127558=DIRECTION ( 'NONE',  ( 0.7071067811865487940, -0.7071067811865463515, 0.000000000000000000 ) ) ;
#127559=DIRECTION ( 'NONE',  ( -0.7071067811865486830, -0.7071067811865464625, 0.000000000000000000 ) ) ;
#127562=LINE ( 'NONE', #94200, #54933 ) ;
#127564=EDGE_LOOP ( 'NONE', ( #63204, #114270, #44768, #57159 ) ) ;
#127565=ORIENTED_EDGE ( 'NONE', *, *, #15736, .F. ) ;
#127566=VECTOR ( 'NONE', #23426, 1000.000000000000227 ) ;
#127567=CARTESIAN_POINT ( 'NONE',  ( -19.49999999999985789, -8.947814304570730570, 5.000000000000000000 ) ) ;
#127568=EDGE_LOOP ( 'NONE', ( #111798, #14465, #73055, #139275 ) ) ;
#127569=EDGE_CURVE ( 'NONE', #34714, #111174, #7624, .T. ) ;
#127570=VERTEX_POINT ( 'NONE', #78452 ) ;
#127572=VECTOR ( 'NONE', #37173, 1000.000000000000000 ) ;
#127573=VECTOR ( 'NONE', #71382, 1000.000000000000000 ) ;
#127574=LINE ( 'NONE', #137023, #12067 ) ;
#127575=PLANE ( 'NONE',  #112066 ) ;
#127577=DIRECTION ( 'NONE',  ( -0.000000000000000000, -0.3543493200069152693, 0.9351131265310292928 ) ) ;
#127578=CYLINDRICAL_SURFACE ( 'NONE', #29314, 0.5000000000000004441 ) ;
#127579=FACE_OUTER_BOUND ( 'NONE', #136781, .T. ) ;
#127581=DIRECTION ( 'NONE',  ( 0.6830127018922181881, 0.6830127018922202975, -0.2588190451025214056 ) ) ;
#127584=LINE ( 'NONE', #106505, #134726 ) ;
#127585=CARTESIAN_POINT ( 'NONE',  ( 36.48921356237310221, -27.52281430457080802, 5.000000000000000000 ) ) ;
#127586=ORIENTED_EDGE ( 'NONE', *, *, #101936, .F. ) ;
#127587=CARTESIAN_POINT ( 'NONE',  ( 25.60343192894627862, -14.24070752338413293, 19.24067776001731644 ) ) ;
#127589=LINE ( 'NONE', #81977, #36506 ) ;
#127590=AXIS2_PLACEMENT_3D ( 'NONE', #9595, #98070, #55287 ) ;
#127591=DIRECTION ( 'NONE',  ( -0.7071067811865486830, 0.7071067811865464625, 0.000000000000000000 ) ) ;
#127592=EDGE_LOOP ( 'NONE', ( #8508, #118496, #77761, #30978 ) ) ;
#127594=ORIENTED_EDGE ( 'NONE', *, *, #113345, .T. ) ;
#127595=ORIENTED_EDGE ( 'NONE', *, *, #79226, .F. ) ;
#127596=ADVANCED_FACE ( 'NONE', ( #89317 ), #51889, .T. ) ;
#127597=VERTEX_POINT ( 'NONE', #45838 ) ;
#127598=ADVANCED_FACE ( 'NONE', ( #87887 ), #11003, .F. ) ;
#127599=EDGE_CURVE ( 'NONE', #110134, #71568, #1550, .T. ) ;
#127601=EDGE_LOOP ( 'NONE', ( #119048, #36093, #55301, #41315 ) ) ;
#127603=CARTESIAN_POINT ( 'NONE',  ( 34.92499999999998295, 10.80009451602706783, 4.759050581649326261 ) ) ;
#127604=DIRECTION ( 'NONE',  ( -0.7071067811865486830, -0.7071067811865464625, -0.000000000000000000 ) ) ;
#127606=LINE ( 'NONE', #50053, #139972 ) ;
#127607=ADVANCED_FACE ( 'NONE', ( #142976 ), #90014, .F. ) ;
#127608=CARTESIAN_POINT ( 'NONE',  ( 25.49999999999982592, -15.29013452822851882, 0.3645803511610929970 ) ) ;
#127609=VECTOR ( 'NONE', #104130, 999.9999999999998863 ) ;
#127611=VECTOR ( 'NONE', #126063, 1000.000000000000000 ) ;
#127612=LINE ( 'NONE', #72564, #84038 ) ;
#127613=ADVANCED_FACE ( 'NONE', ( #76311 ), #120472, .F. ) ;
#127615=PLANE ( 'NONE',  #96889 ) ;
#127616=DIRECTION ( 'NONE',  ( 0.6830127018922180770, -0.6830127018922204085, -0.2588190451025213501 ) ) ;
#127617=EDGE_LOOP ( 'NONE', ( #13980, #114241, #5263, #83969 ) ) ;
#127618=EDGE_LOOP ( 'NONE', ( #111183, #133864, #79018, #35836 ) ) ;
#127620=VECTOR ( 'NONE', #126906, 999.9999999999998863 ) ;
#127621=VERTEX_POINT ( 'NONE', #98745 ) ;
#127622=CARTESIAN_POINT ( 'NONE',  ( 23.20710678118638981, 18.75929247661552779, 5.000000000000000000 ) ) ;
#127623=EDGE_CURVE ( 'NONE', #15696, #49015, #43671, .T. ) ;
#127624=VERTEX_POINT ( 'NONE', #37068 ) ;
#127625=ORIENTED_EDGE ( 'NONE', *, *, #51628, .T. ) ;
#127626=FACE_OUTER_BOUND ( 'NONE', #42481, .T. ) ;
#127628=CARTESIAN_POINT ( 'NONE',  ( 21.79996877983149517, 8.259292476615627265, 16.85664084051835943 ) ) ;
#127629=ORIENTED_EDGE ( 'NONE', *, *, #95395, .F. ) ;
#127630=FACE_OUTER_BOUND ( 'NONE', #33989, .T. ) ;
#127631=EDGE_CURVE ( 'NONE', #92458, #91018, #81321, .T. ) ;
#127632=VECTOR ( 'NONE', #22467, 999.9999999999998863 ) ;
#127633=VERTEX_POINT ( 'NONE', #124090 ) ;
#127635=DIRECTION ( 'NONE',  ( 0.7071067811865487940, 0.7071067811865463515, -0.000000000000000000 ) ) ;
#127637=ORIENTED_EDGE ( 'NONE', *, *, #98828, .F. ) ;
#127639=PLANE ( 'NONE',  #107792 ) ;
#127640=( BOUNDED_CURVE ( )  B_SPLINE_CURVE ( 3, ( #25163, #13559, #4073, #24458 ),
 .UNSPECIFIED., .F., .T. ) 
 B_SPLINE_CURVE_WITH_KNOTS ( ( 4, 4 ),
 ( 5.043186909253412509, 5.074607125596365620 ),
 .UNSPECIFIED. ) 
 CURVE ( )  GEOMETRIC_REPRESENTATION_ITEM ( )  RATIONAL_B_SPLINE_CURVE ( ( 1.000000000000000000, 0.9999177325257868620, 0.9999177325257868620, 1.000000000000000000 ) ) 
 REPRESENTATION_ITEM ( '' )  );
#127641=DIRECTION ( 'NONE',  ( -0.000000000000000000, 0.000000000000000000, 1.000000000000000000 ) ) ;
#127644=ORIENTED_EDGE ( 'NONE', *, *, #35424, .T. ) ;
#127645=DIRECTION ( 'NONE',  ( 0.6830127018922180770, -0.6830127018922204085, -0.2588190451025213501 ) ) ;
#127646=ORIENTED_EDGE ( 'NONE', *, *, #17802, .F. ) ;
#127647=CARTESIAN_POINT ( 'NONE',  ( 30.29974487139158867, -27.71228299555227537, 4.000000000000000000 ) ) ;
#127649=FACE_OUTER_BOUND ( 'NONE', #122663, .T. ) ;
#127651=ADVANCED_FACE ( 'NONE', ( #27612 ), #5118, .F. ) ;
#127652=VECTOR ( 'NONE', #124927, 1000.000000000000000 ) ;
#127653=ADVANCED_FACE ( 'NONE', ( #60281 ), #126230, .F. ) ;
#127654=CARTESIAN_POINT ( 'NONE',  ( 14.99451991528749595, 28.92564299267948513, 4.000000000000000000 ) ) ;
#127655=VECTOR ( 'NONE', #43249, 1000.000000000000000 ) ;
#127657=CARTESIAN_POINT ( 'NONE',  ( -31.49999999999978684, -9.462702396501040170, -9.474982329943443915 ) ) ;
#127658=VERTEX_POINT ( 'NONE', #37813 ) ;
#127659=CARTESIAN_POINT ( 'NONE',  ( 20.99451991528748707, 28.92564299267952777, 4.000000000000000000 ) ) ;
#127660=VECTOR ( 'NONE', #13681, 1000.000000000000000 ) ;
#127661=AXIS2_PLACEMENT_3D ( 'NONE', #76708, #139824, #120879 ) ;
#127662=AXIS2_PLACEMENT_3D ( 'NONE', #2152, #136270, #46459 ) ;
#127663=LINE ( 'NONE', #116044, #88745 ) ;
#127664=ADVANCED_FACE ( 'NONE', ( #79918 ), #69012, .F. ) ;
#127666=ORIENTED_EDGE ( 'NONE', *, *, #95210, .T. ) ;
#127668=VERTEX_POINT ( 'NONE', #113920 ) ;
#127669=ADVANCED_FACE ( 'NONE', ( #82732 ), #15281, .F. ) ;
#127670=ORIENTED_EDGE ( 'NONE', *, *, #140388, .T. ) ;
#127672=VECTOR ( 'NONE', #90840, 1000.000000000000000 ) ;
#127673=DIRECTION ( 'NONE',  ( -0.7071067811865487940, 0.7071067811865463515, 0.000000000000000000 ) ) ;
#127674=ORIENTED_EDGE ( 'NONE', *, *, #17580, .F. ) ;
#127675=CARTESIAN_POINT ( 'NONE',  ( -15.29974487139158867, -27.71228299555216879, 4.000000000000000000 ) ) ;
#127676=DIRECTION ( 'NONE',  ( 0.7071067811865487940, 0.7071067811865463515, -0.000000000000000000 ) ) ;
#127677=DIRECTION ( 'NONE',  ( 0.3543493200069162685, -0.000000000000000000, -0.9351131265310288487 ) ) ;
#127678=ORIENTED_EDGE ( 'NONE', *, *, #24448, .T. ) ;
#127679=VECTOR ( 'NONE', #52147, 1000.000000000000000 ) ;
#127680=ADVANCED_FACE ( 'NONE', ( #69742 ), #135685, .F. ) ;
#127681=LINE ( 'NONE', #30506, #2126 ) ;
#127682=PLANE ( 'NONE',  #58206 ) ;
#127683=CARTESIAN_POINT ( 'NONE',  ( 26.67183060077628909, 17.25929247661554555, 4.000000000000000000 ) ) ;
#127684=DIRECTION ( 'NONE',  ( 0.7071067811865487940, 0.7071067811865463515, -0.000000000000000000 ) ) ;
#127685=CARTESIAN_POINT ( 'NONE',  ( -39.29974487139159578, -27.71228299555233576, 4.000000000000000000 ) ) ;
#127686=CARTESIAN_POINT ( 'NONE',  ( -25.96836484077792306, 2.259292476615697876, 13.77329220150631173 ) ) ;
#127688=EDGE_CURVE ( 'NONE', #135612, #119750, #103048, .T. ) ;
#127689=PLANE ( 'NONE',  #78976 ) ;
#127692=ORIENTED_EDGE ( 'NONE', *, *, #71039, .T. ) ;
#127693=EDGE_LOOP ( 'NONE', ( #30959, #12088, #56254, #62895 ) ) ;
#127695=AXIS2_PLACEMENT_3D ( 'NONE', #73033, #128794, #117185 ) ;
#127696=ORIENTED_EDGE ( 'NONE', *, *, #116268, .T. ) ;
#127699=ORIENTED_EDGE ( 'NONE', *, *, #59560, .F. ) ;
#127700=DIRECTION ( 'NONE',  ( 0.3543493200069162685, -0.000000000000000000, -0.9351131265310288487 ) ) ;
#127701=VECTOR ( 'NONE', #14460, 1000.000000000000000 ) ;
#127702=EDGE_LOOP ( 'NONE', ( #75176, #97480, #51669, #31501 ) ) ;
#127703=DIRECTION ( 'NONE',  ( -0.000000000000000000, 0.000000000000000000, 1.000000000000000000 ) ) ;
#127705=CARTESIAN_POINT ( 'NONE',  ( 11.99999999999991296, 20.70535890316562444, 1.956823837851888959 ) ) ;
#127708=VECTOR ( 'NONE', #27832, 1000.000000000000000 ) ;
#127709=ORIENTED_EDGE ( 'NONE', *, *, #123711, .F. ) ;
#127710=CARTESIAN_POINT ( 'NONE',  ( -38.99451991528749062, 28.92564299267965211, 4.000000000000000000 ) ) ;
#127711=CARTESIAN_POINT ( 'NONE',  ( -54.18398860626899705, 28.73617430169825226, 5.000000000000000000 ) ) ;
#127712=CARTESIAN_POINT ( 'NONE',  ( 8.207106781186489286, -11.24070752338417023, 5.000000000000000000 ) ) ;
#127713=CARTESIAN_POINT ( 'NONE',  ( 8.999999999999937828, 9.631307414974335401, -9.079085613539522370 ) ) ;
#127715=CARTESIAN_POINT ( 'NONE',  ( 15.18398860626900237, 28.73617430169797871, 5.000000000000000000 ) ) ;
#127718=( BOUNDED_CURVE ( )  B_SPLINE_CURVE ( 3, ( #128726, #18503, #63508, #107675 ),
 .UNSPECIFIED., .F., .T. ) 
 B_SPLINE_CURVE_WITH_KNOTS ( ( 4, 4 ),
 ( 1.964434688349488978, 3.503810798801449522 ),
 .UNSPECIFIED. ) 
 CURVE ( )  GEOMETRIC_REPRESENTATION_ITEM ( )  RATIONAL_B_SPLINE_CURVE ( ( 1.000000000000000000, 0.8120851936182288400, 0.8120851936182288400, 1.000000000000000000 ) ) 
 REPRESENTATION_ITEM ( '' )  );
#127719=LINE ( 'NONE', #92196, #81458 ) ;
#127720=EDGE_CURVE ( 'NONE', #60449, #31525, #57425, .T. ) ;
#127721=CARTESIAN_POINT ( 'NONE',  ( -2.916851932270679626, 21.75929247661549581, 7.311836541448045068 ) ) ;
#127722=EDGE_LOOP ( 'NONE', ( #81546, #37090, #99043, #82461 ) ) ;
#127723=ORIENTED_EDGE ( 'NONE', *, *, #43465, .T. ) ;
#127726=LINE ( 'NONE', #28406, #9263 ) ;
#127728=CARTESIAN_POINT ( 'NONE',  ( -12.32816939922345334, 14.25929247661557753, 4.000000000000000000 ) ) ;
#127729=VECTOR ( 'NONE', #18149, 1000.000000000000227 ) ;
#127730=PLANE ( 'NONE',  #119673 ) ;
#127731=DIRECTION ( 'NONE',  ( -0.000000000000000000, -0.3543493200069152693, 0.9351131265310292928 ) ) ;
#127732=PLANE ( 'NONE',  #72180 ) ;
#127733=DIRECTION ( 'NONE',  ( -0.000000000000000000, 0.3543493200069153248, 0.9351131265310292928 ) ) ;
#127735=VERTEX_POINT ( 'NONE', #4371 ) ;
#127737=DIRECTION ( 'NONE',  ( 0.7071067811865486830, -0.7071067811865464625, -0.000000000000000000 ) ) ;
#127739=AXIS2_PLACEMENT_3D ( 'NONE', #102353, #101600, #66851 ) ;
#127740=DIRECTION ( 'NONE',  ( 0.6830127018922181881, 0.6830127018922202975, -0.2588190451025214056 ) ) ;
#127741=CARTESIAN_POINT ( 'NONE',  ( -26.48334561358936412, 22.22500000000000142, 4.500000000000000888 ) ) ;
#127743=ORIENTED_EDGE ( 'NONE', *, *, #40251, .F. ) ;
#127745=ORIENTED_EDGE ( 'NONE', *, *, #74108, .T. ) ;
#127746=DIRECTION ( 'NONE',  ( -0.7071067811865486830, -0.7071067811865464625, -0.000000000000000000 ) ) ;
#127747=LINE ( 'NONE', #84261, #39221 ) ;
#127748=DIRECTION ( 'NONE',  ( 0.6830127018922180770, -0.6830127018922204085, -0.2588190451025213501 ) ) ;
#127749=CARTESIAN_POINT ( 'NONE',  ( 5.999999999999956479, -4.068876922607770119, 4.000000000000000000 ) ) ;
#127750=VECTOR ( 'NONE', #19617, 1000.000000000000000 ) ;
#127752=ORIENTED_EDGE ( 'NONE', *, *, #103378, .T. ) ;
#127754=CARTESIAN_POINT ( 'NONE',  ( -65.99451991528749772, 28.92564299267984396, 4.000000000000000000 ) ) ;
#127756=ORIENTED_EDGE ( 'NONE', *, *, #74778, .F. ) ;
#127758=VECTOR ( 'NONE', #40313, 1000.000000000000227 ) ;
#127759=VECTOR ( 'NONE', #34924, 1000.000000000000000 ) ;
#127760=ORIENTED_EDGE ( 'NONE', *, *, #55378, .F. ) ;
#127763=DIRECTION ( 'NONE',  ( 0.6830127018922181881, 0.6830127018922202975, -0.2588190451025214056 ) ) ;
#127764=EDGE_LOOP ( 'NONE', ( #90229, #118783, #89899, #142838 ) ) ;
#127768=CARTESIAN_POINT ( 'NONE',  ( 0.000000000000000000, 0.000000000000000000, 5.000000000000000000 ) ) ;
#127769=EDGE_CURVE ( 'NONE', #20060, #22051, #48673, .T. ) ;
#127770=FACE_BOUND ( 'NONE', #118378, .T. ) ;
#127771=LINE ( 'NONE', #28460, #50353 ) ;
#127772=EDGE_CURVE ( 'NONE', #52005, #63170, #24766, .T. ) ;
#127773=ADVANCED_FACE ( 'NONE', ( #112496 ), #124797, .F. ) ;
#127774=PLANE ( 'NONE',  #130139 ) ;
#127777=CARTESIAN_POINT ( 'NONE',  ( 33.18398860626899705, 28.73617430169810305, 5.000000000000000000 ) ) ;
#127778=CARTESIAN_POINT ( 'NONE',  ( 53.99451991528749062, 28.92564299267975869, 4.000000000000000000 ) ) ;
#127779=ORIENTED_EDGE ( 'NONE', *, *, #143093, .F. ) ;
#127780=ORIENTED_EDGE ( 'NONE', *, *, #102614, .F. ) ;
#127781=PLANE ( 'NONE',  #121221 ) ;
#127783=EDGE_CURVE ( 'NONE', #26300, #73694, #13153, .T. ) ;
#127784=ADVANCED_FACE ( 'NONE', ( #134994 ), #6528, .F. ) ;
#127785=ORIENTED_EDGE ( 'NONE', *, *, #55588, .F. ) ;
#127787=VERTEX_POINT ( 'NONE', #63842 ) ;
#127788=DIRECTION ( 'NONE',  ( -0.7071067811865486830, -0.7071067811865464625, -0.000000000000000000 ) ) ;
#127790=ADVANCED_FACE ( 'NONE', ( #51540 ), #16745, .F. ) ;
#127791=ORIENTED_EDGE ( 'NONE', *, *, #20418, .T. ) ;
#127794=VECTOR ( 'NONE', #56326, 1000.000000000000227 ) ;
#127795=ADVANCED_FACE ( 'NONE', ( #83447 ), #129786, .F. ) ;
#127796=AXIS2_PLACEMENT_3D ( 'NONE', #51808, #85121, #61292 ) ;
#127797=LINE ( 'NONE', #125653, #17714 ) ;
#127798=CARTESIAN_POINT ( 'NONE',  ( -14.22995720542196985, 21.73644205237998150, 5.000000000000000888 ) ) ;
#127799=VECTOR ( 'NONE', #71119, 1000.000000000000000 ) ;
#127802=ORIENTED_EDGE ( 'NONE', *, *, #83613, .F. ) ;
#127803=ORIENTED_EDGE ( 'NONE', *, *, #26982, .F. ) ;
#127806=LINE ( 'NONE', #105999, #74467 ) ;
#127807=VERTEX_POINT ( 'NONE', #140653 ) ;
#127808=ADVANCED_FACE ( 'NONE', ( #39226 ), #28353, .F. ) ;
#127809=ORIENTED_EDGE ( 'NONE', *, *, #136683, .F. ) ;
#127810=ORIENTED_EDGE ( 'NONE', *, *, #141269, .F. ) ;
#127811=DIRECTION ( 'NONE',  ( -0.6830127018922180770, -0.6830127018922204085, -0.2588190451025213501 ) ) ;
#127813=LINE ( 'NONE', #47433, #64737 ) ;
#127814=ORIENTED_EDGE ( 'NONE', *, *, #125227, .T. ) ;
#127815=LINE ( 'NONE', #91598, #108749 ) ;
#127816=EDGE_CURVE ( 'NONE', #94981, #47967, #107318, .T. ) ;
#127817=AXIS2_PLACEMENT_3D ( 'NONE', #121338, #122768, #2385 ) ;
#127820=CARTESIAN_POINT ( 'NONE',  ( 51.18398860626899705, 28.73617430169823095, 5.000000000000000000 ) ) ;
#127823=DIRECTION ( 'NONE',  ( -0.3543493200069162685, -0.000000000000000000, -0.9351131265310288487 ) ) ;
#127826=DIRECTION ( 'NONE',  ( 0.000000000000000000, 0.000000000000000000, -1.000000000000000000 ) ) ;
#127827=LINE ( 'NONE', #5284, #19103 ) ;
#127828=ORIENTED_EDGE ( 'NONE', *, *, #23476, .F. ) ;
#127829=FACE_OUTER_BOUND ( 'NONE', #110792, .T. ) ;
#127830=AXIS2_PLACEMENT_3D ( 'NONE', #128225, #139834, #141211 ) ;
#127831=ORIENTED_EDGE ( 'NONE', *, *, #49890, .F. ) ;
#127832=CARTESIAN_POINT ( 'NONE',  ( -1.499999999999994449, -1.592773361805376098, -6.492772025301226435 ) ) ;
#127834=LINE ( 'NONE', #26367, #10007 ) ;
#127837=EDGE_CURVE ( 'NONE', #112904, #111757, #7988, .T. ) ;
#127838=PLANE ( 'NONE',  #44977 ) ;
#127839=FACE_OUTER_BOUND ( 'NONE', #89083, .T. ) ;
#127840=DIRECTION ( 'NONE',  ( -0.7071067811865486830, -0.7071067811865464625, 0.000000000000000000 ) ) ;
#127841=VECTOR ( 'NONE', #33534, 1000.000000000000227 ) ;
#127842=VERTEX_POINT ( 'NONE', #105178 ) ;
#127843=CARTESIAN_POINT ( 'NONE',  ( 8.999999999999941380, -12.41253812416062985, 4.000000000000000000 ) ) ;
#127844=DIRECTION ( 'NONE',  ( 0.7071067811865487940, 0.7071067811865463515, -0.000000000000000000 ) ) ;
#127845=DIRECTION ( 'NONE',  ( -0.7071067811865486830, -0.7071067811865464625, 0.000000000000000000 ) ) ;
#127846=EDGE_CURVE ( 'NONE', #2765, #72157, #94996, .T. ) ;
#127847=DIRECTION ( 'NONE',  ( -0.7071067811865487940, 0.7071067811865463515, 0.000000000000000000 ) ) ;
#127851=VECTOR ( 'NONE', #28026, 1000.000000000000000 ) ;
#127856=DIRECTION ( 'NONE',  ( 0.7071067811865487940, 0.7071067811865463515, -0.000000000000000000 ) ) ;
#127857=LINE ( 'NONE', #127104, #36884 ) ;
#127858=CARTESIAN_POINT ( 'NONE',  ( 34.49999999999975842, -13.53574439159937093, 4.994342998332162331 ) ) ;
#127859=PLANE ( 'NONE',  #109313 ) ;
#127860=ORIENTED_EDGE ( 'NONE', *, *, #20189, .F. ) ;
#127861=EDGE_CURVE ( 'NONE', #20060, #86073, #138538, .T. ) ;
#127862=PLANE ( 'NONE',  #9363 ) ;
#127865=VECTOR ( 'NONE', #77924, 1000.000000000000000 ) ;
#127866=VECTOR ( 'NONE', #134796, 1000.000000000000000 ) ;
#127867=VECTOR ( 'NONE', #66763, 1000.000000000000000 ) ;
#127868=LINE ( 'NONE', #72805, #126982 ) ;
#127871=VECTOR ( 'NONE', #101046, 1000.000000000000000 ) ;
#127872=VECTOR ( 'NONE', #117389, 999.9999999999998863 ) ;
#127875=ORIENTED_EDGE ( 'NONE', *, *, #107287, .F. ) ;
#127876=ORIENTED_EDGE ( 'NONE', *, *, #70818, .F. ) ;
#127878=AXIS2_PLACEMENT_3D ( 'NONE', #62622, #18345, #106801 ) ;
#127880=AXIS2_PLACEMENT_3D ( 'NONE', #8925, #141658, #53195 ) ;
#127881=CARTESIAN_POINT ( 'NONE',  ( -1.628234450443837744, -8.240707523384200428, 11.38925528200752879 ) ) ;
#127883=CARTESIAN_POINT ( 'NONE',  ( -60.29974487139158867, -27.71228299555248142, 4.000000000000000000 ) ) ;
#127885=FACE_OUTER_BOUND ( 'NONE', #117315, .T. ) ;
#127887=DIRECTION ( 'NONE',  ( -0.7071067811865486830, -0.7071067811865464625, 0.000000000000000000 ) ) ;
#127888=DIRECTION ( 'NONE',  ( -0.000000000000000000, -0.3543493200069152693, 0.9351131265310292928 ) ) ;
#127890=CARTESIAN_POINT ( 'NONE',  ( -48.18398860626899705, 28.73617430169820608, 5.000000000000000000 ) ) ;
#127891=LINE ( 'NONE', #130011, #71273 ) ;
#127893=CARTESIAN_POINT ( 'NONE',  ( 72.48921356237309510, -27.52281430457106026, 5.000000000000000000 ) ) ;
#127894=VERTEX_POINT ( 'NONE', #95733 ) ;
#127895=ORIENTED_EDGE ( 'NONE', *, *, #62018, .F. ) ;
#127897=PLANE ( 'NONE',  #125757 ) ;
#127898=CARTESIAN_POINT ( 'NONE',  ( 0.000000000000000000, 0.000000000000000000, 5.000000000000000000 ) ) ;
#127899=PLANE ( 'NONE',  #129426 ) ;
#127900=EDGE_LOOP ( 'NONE', ( #75579, #99799, #133306, #87904 ) ) ;
#127901=EDGE_CURVE ( 'NONE', #90863, #32826, #139981, .T. ) ;
#127904=ADVANCED_FACE ( 'NONE', ( #42809 ), #89154, .F. ) ;
#127907=VECTOR ( 'NONE', #122254, 1000.000000000000000 ) ;
#127908=EDGE_LOOP ( 'NONE', ( #130916, #133956, #93392, #38572 ) ) ;
#127909=CARTESIAN_POINT ( 'NONE',  ( 8.999999999999952038, 20.58746187583903264, 4.000000000000000000 ) ) ;
#127910=ORIENTED_EDGE ( 'NONE', *, *, #74482, .F. ) ;
#127911=ORIENTED_EDGE ( 'NONE', *, *, #84935, .T. ) ;
#127913=CARTESIAN_POINT ( 'NONE',  ( 29.99999999999979394, 12.83542986846999945, -1.025386466790438433 ) ) ;
#127914=DIRECTION ( 'NONE',  ( 0.7071067811865487940, 0.7071067811865463515, -0.000000000000000000 ) ) ;
#127916=EDGE_CURVE ( 'NONE', #106511, #43627, #56572, .T. ) ;
#127917=FACE_OUTER_BOUND ( 'NONE', #116541, .T. ) ;
#127919=EDGE_LOOP ( 'NONE', ( #15913, #129816, #17572, #102635 ) ) ;
#127920=DIRECTION ( 'NONE',  ( -0.000000000000000000, -0.3543493200069152693, 0.9351131265310292928 ) ) ;
#127921=DIRECTION ( 'NONE',  ( 1.000000000000000000, 0.000000000000000000, 0.000000000000000000 ) ) ;
#127922=CARTESIAN_POINT ( 'NONE',  ( -36.29974487139159578, -27.71228299555231445, 4.000000000000000000 ) ) ;
#127924=ORIENTED_EDGE ( 'NONE', *, *, #108867, .F. ) ;
#127925=ORIENTED_EDGE ( 'NONE', *, *, #101122, .F. ) ;
#127926=DIRECTION ( 'NONE',  ( 0.7071067811865487940, 0.7071067811865463515, 0.000000000000000000 ) ) ;
#127927=CARTESIAN_POINT ( 'NONE',  ( 30.48921356237309510, -27.52281430457076894, 5.000000000000000000 ) ) ;
#127928=CARTESIAN_POINT ( 'NONE',  ( -25.49999999999982236, 18.05218569542898521, 5.000000000000000000 ) ) ;
#127929=VECTOR ( 'NONE', #77312, 999.9999999999998863 ) ;
#127930=CARTESIAN_POINT ( 'NONE',  ( -28.11017322888191217, -22.22500000000000142, 4.785647885939352086 ) ) ;
#127931=ORIENTED_EDGE ( 'NONE', *, *, #118690, .F. ) ;
#127932=VERTEX_POINT ( 'NONE', #34069 ) ;
#127934=CARTESIAN_POINT ( 'NONE',  ( -32.38161509397984616, -2.240707523384260824, 13.37739548510246834 ) ) ;
#127936=ORIENTED_EDGE ( 'NONE', *, *, #114977, .F. ) ;
#127937=( BOUNDED_CURVE ( )  B_SPLINE_CURVE ( 3, ( #26665, #102094, #92614, #4124 ),
 .UNSPECIFIED., .F., .F. ) 
 B_SPLINE_CURVE_WITH_KNOTS ( ( 4, 4 ),
 ( 2.779374508378134045, 4.199602562396839822 ),
 .UNSPECIFIED. ) 
 CURVE ( )  GEOMETRIC_REPRESENTATION_ITEM ( )  RATIONAL_B_SPLINE_CURVE ( ( 1.000000000000000000, 0.8388583629366623828, 0.8388583629366623828, 1.000000000000000000 ) ) 
 REPRESENTATION_ITEM ( '' )  );
#127939=CARTESIAN_POINT ( 'NONE',  ( -19.25154412867563636, -11.24070752338416845, 10.39518518046013718 ) ) ;
#127940=ORIENTED_EDGE ( 'NONE', *, *, #43133, .T. ) ;
#127941=CARTESIAN_POINT ( 'NONE',  ( 0.000000000000000000, -21.72500000000000142, 4.500000000000000888 ) ) ;
#127942=LINE ( 'NONE', #112511, #19263 ) ;
#127943=VECTOR ( 'NONE', #19494, 999.9999999999998863 ) ;
#127944=( BOUNDED_CURVE ( )  B_SPLINE_CURVE ( 3, ( #116896, #17567, #61831, #105991 ),
 .UNSPECIFIED., .F., .T. ) 
 B_SPLINE_CURVE_WITH_KNOTS ( ( 4, 4 ),
 ( 3.101920907804236460, 3.199716232068803290 ),
 .UNSPECIFIED. ) 
 CURVE ( )  GEOMETRIC_REPRESENTATION_ITEM ( )  RATIONAL_B_SPLINE_CURVE ( ( 1.000000000000000000, 0.9992031649997842324, 0.9992031649997842324, 1.000000000000000000 ) ) 
 REPRESENTATION_ITEM ( '' )  );
#127945=FACE_BOUND ( 'NONE', #14850, .T. ) ;
#127948=DIRECTION ( 'NONE',  ( 0.6830127018922180770, -0.6830127018922204085, -0.2588190451025213501 ) ) ;
#127949=VECTOR ( 'NONE', #115179, 1000.000000000000000 ) ;
#127950=LINE ( 'NONE', #139558, #41243 ) ;
#127951=ORIENTED_EDGE ( 'NONE', *, *, #106620, .F. ) ;
#127954=ORIENTED_EDGE ( 'NONE', *, *, #83613, .T. ) ;
#127955=ADVANCED_FACE ( 'NONE', ( #23135 ), #77581, .F. ) ;
#127956=EDGE_CURVE ( 'NONE', #39694, #62221, #20294, .T. ) ;
#127957=VERTEX_POINT ( 'NONE', #122467 ) ;
#127959=EDGE_LOOP ( 'NONE', ( #139755, #126189, #28003, #20094 ) ) ;
#127960=EDGE_CURVE ( 'NONE', #16274, #128301, #121048, .T. ) ;
#127961=LINE ( 'NONE', #50389, #81332 ) ;
#127962=EDGE_CURVE ( 'NONE', #467, #28420, #54407, .T. ) ;
#127963=DIRECTION ( 'NONE',  ( 0.7071067811865486830, -0.7071067811865464625, -0.000000000000000000 ) ) ;
#127964=VECTOR ( 'NONE', #141563, 1000.000000000000227 ) ;
#127965=VECTOR ( 'NONE', #71586, 1000.000000000000227 ) ;
#127966=EDGE_CURVE ( 'NONE', #6023, #33545, #33381, .T. ) ;
#127967=PLANE ( 'NONE',  #73448 ) ;
#127968=VECTOR ( 'NONE', #65443, 1000.000000000000227 ) ;
#127970=CARTESIAN_POINT ( 'NONE',  ( -34.92500000000001137, 22.22500000000000142, 4.000000000000000000 ) ) ;
#127971=ORIENTED_EDGE ( 'NONE', *, *, #50180, .T. ) ;
#127972=DIRECTION ( 'NONE',  ( 0.7071067811865486830, -0.7071067811865464625, -0.000000000000000000 ) ) ;
#127973=EDGE_CURVE ( 'NONE', #38542, #91904, #686, .T. ) ;
#127974=CARTESIAN_POINT ( 'NONE',  ( -36.18398860626899705, 28.73617430169812437, 5.000000000000000000 ) ) ;
#127975=DIRECTION ( 'NONE',  ( -0.000000000000000000, 0.000000000000000000, 1.000000000000000000 ) ) ;
#127976=DIRECTION ( 'NONE',  ( -0.7071067811865487940, 0.7071067811865463515, 0.000000000000000000 ) ) ;
#127977=CARTESIAN_POINT ( 'NONE',  ( 39.18398860626899705, 28.73617430169814568, 5.000000000000000000 ) ) ;
#127978=DIRECTION ( 'NONE',  ( 0.7071067811865486830, -0.7071067811865464625, -0.000000000000000000 ) ) ;
#127979=VECTOR ( 'NONE', #100257, 1000.000000000000000 ) ;
#127980=VECTOR ( 'NONE', #94689, 1000.000000000000000 ) ;
#127982=DIRECTION ( 'NONE',  ( -0.3543493200069163240, 0.000000000000000000, 0.9351131265310288487 ) ) ;
#127983=EDGE_LOOP ( 'NONE', ( #25437, #70918, #139870, #59999, #130294 ) ) ;
#127984=FACE_OUTER_BOUND ( 'NONE', #62877, .T. ) ;
#127985=DIRECTION ( 'NONE',  ( 0.6830127018922181881, 0.6830127018922202975, -0.2588190451025214056 ) ) ;
#127986=EDGE_CURVE ( 'NONE', #119991, #38500, #121749, .T. ) ;
#127987=ORIENTED_EDGE ( 'NONE', *, *, #124988, .F. ) ;
#127988=ORIENTED_EDGE ( 'NONE', *, *, #58497, .F. ) ;
#127989=EDGE_CURVE ( 'NONE', #63130, #138721, #22427, .T. ) ;
#127990=EDGE_LOOP ( 'NONE', ( #113519, #89309, #137496, #131021 ) ) ;
#127992=ORIENTED_EDGE ( 'NONE', *, *, #17137, .F. ) ;
#127993=EDGE_CURVE ( 'NONE', #30706, #102869, #12286, .T. ) ;
#127994=VECTOR ( 'NONE', #137304, 999.9999999999998863 ) ;
#127997=DIRECTION ( 'NONE',  ( -0.000000000000000000, 0.000000000000000000, 1.000000000000000000 ) ) ;
#127998=ORIENTED_EDGE ( 'NONE', *, *, #140831, .T. ) ;
#127999=LINE ( 'NONE', #106184, #115929 ) ;
#128000=LINE ( 'NONE', #3991, #89207 ) ;
#128002=EDGE_LOOP ( 'NONE', ( #94000, #113148, #86214, #117776 ) ) ;
#128003=ORIENTED_EDGE ( 'NONE', *, *, #128754, .F. ) ;
#128004=FACE_OUTER_BOUND ( 'NONE', #85893, .T. ) ;
#128007=EDGE_LOOP ( 'NONE', ( #30639, #141825, #142964, #91392 ) ) ;
#128008=CARTESIAN_POINT ( 'NONE',  ( -39.18398860626899705, 28.73617430169814568, 5.000000000000000000 ) ) ;
#128009=ORIENTED_EDGE ( 'NONE', *, *, #121882, .T. ) ;
#128011=VECTOR ( 'NONE', #40138, 1000.000000000000000 ) ;
#128014=EDGE_CURVE ( 'NONE', #93893, #117034, #143519, .T. ) ;
#128015=DIRECTION ( 'NONE',  ( -0.7071067811865486830, -0.7071067811865464625, 0.000000000000000000 ) ) ;
#128016=VECTOR ( 'NONE', #111101, 1000.000000000000227 ) ;
#128017=VECTOR ( 'NONE', #47702, 1000.000000000000000 ) ;
#128018=CARTESIAN_POINT ( 'NONE',  ( -3.489213562373097322, -27.52281430457057709, 5.000000000000000000 ) ) ;
#128019=CARTESIAN_POINT ( 'NONE',  ( -24.84463820744543838, 1.742823668393624903, 4.000000000000000000 ) ) ;
#128020=DIRECTION ( 'NONE',  ( -0.000000000000000000, -0.3543493200069152693, 0.9351131265310292928 ) ) ;
#128021=EDGE_LOOP ( 'NONE', ( #120129, #46843, #22084, #70417 ) ) ;
#128022=FACE_OUTER_BOUND ( 'NONE', #131536, .T. ) ;
#128023=EDGE_LOOP ( 'NONE', ( #19350, #85062, #27786, #64850 ) ) ;
#128024=DIRECTION ( 'NONE',  ( 0.7071067811865486830, -0.7071067811865464625, -0.000000000000000000 ) ) ;
#128026=AXIS2_PLACEMENT_3D ( 'NONE', #689, #34072, #21755 ) ;
#128028=CARTESIAN_POINT ( 'NONE',  ( 27.48921356237309155, -27.52281430457074762, 5.000000000000000000 ) ) ;
#128029=DIRECTION ( 'NONE',  ( 0.7071067811865486830, -0.7071067811865464625, -0.000000000000000000 ) ) ;
#128030=ORIENTED_EDGE ( 'NONE', *, *, #27693, .T. ) ;
#128031=ORIENTED_EDGE ( 'NONE', *, *, #54152, .T. ) ;
#128032=ADVANCED_FACE ( 'NONE', ( #53684 ), #11546, .F. ) ;
#128033=AXIS2_PLACEMENT_3D ( 'NONE', #133137, #121500, #1823 ) ;
#128035=CARTESIAN_POINT ( 'NONE',  ( 34.49999999999975842, 14.14708470758594139, -0.5283514160167365192 ) ) ;
#128036=PLANE ( 'NONE',  #2507 ) ;
#128037=DIRECTION ( 'NONE',  ( -0.000000000000000000, -0.000000000000000000, -1.000000000000000000 ) ) ;
#128038=VECTOR ( 'NONE', #95951, 1000.000000000000000 ) ;
#128039=CARTESIAN_POINT ( 'NONE',  ( -5.999999999999956479, 16.93112307739201583, 4.000000000000000000 ) ) ;
#128042=PLANE ( 'NONE',  #32498 ) ;
#128043=CARTESIAN_POINT ( 'NONE',  ( -8.708222910169469699, -15.74070752338412404, 19.73771281079095630 ) ) ;
#128046=DIRECTION ( 'NONE',  ( 0.7071067811865487940, 0.7071067811865463515, -0.000000000000000000 ) ) ;
#128047=DIRECTION ( 'NONE',  ( 0.7071067811865486830, -0.7071067811865464625, -0.000000000000000000 ) ) ;
#128048=ORIENTED_EDGE ( 'NONE', *, *, #138657, .F. ) ;
#128049=CARTESIAN_POINT ( 'NONE',  ( -26.20710678118635784, 9.759292476615618384, 5.000000000000000000 ) ) ;
#128050=ORIENTED_EDGE ( 'NONE', *, *, #119679, .T. ) ;
#128051=FACE_OUTER_BOUND ( 'NONE', #126313, .T. ) ;
#128053=ORIENTED_EDGE ( 'NONE', *, *, #116, .F. ) ;
#128054=EDGE_CURVE ( 'NONE', #100921, #65559, #76135, .T. ) ;
#128055=CARTESIAN_POINT ( 'NONE',  ( -24.48921356237309510, -27.52281430457072631, 5.000000000000000000 ) ) ;
#128056=PLANE ( 'NONE',  #135185 ) ;
#128057=VERTEX_POINT ( 'NONE', #100035 ) ;
#128059=EDGE_LOOP ( 'NONE', ( #28703, #35586, #100771, #64069 ) ) ;
#128061=CARTESIAN_POINT ( 'NONE',  ( -17.67183060077635659, 20.25929247661551713, 4.000000000000000000 ) ) ;
#128062=CARTESIAN_POINT ( 'NONE',  ( -62.99451991528749772, 28.92564299267982264, 4.000000000000000000 ) ) ;
#128064=DIRECTION ( 'NONE',  ( 0.3543493200069162685, -0.000000000000000000, -0.9351131265310288487 ) ) ;
#128065=EDGE_CURVE ( 'NONE', #288, #138468, #94925, .T. ) ;
#128066=CARTESIAN_POINT ( 'NONE',  ( -33.70710678118631165, 17.25929247661554911, 5.000000000000000000 ) ) ;
#128067=VERTEX_POINT ( 'NONE', #113748 ) ;
#128068=LINE ( 'NONE', #128753, #139544 ) ;
#128071=VECTOR ( 'NONE', #128377, 1000.000000000000000 ) ;
#128073=ORIENTED_EDGE ( 'NONE', *, *, #16701, .F. ) ;
#128074=VECTOR ( 'NONE', #89273, 1000.000000000000000 ) ;
#128076=ORIENTED_EDGE ( 'NONE', *, *, #26656, .F. ) ;
#128077=EDGE_CURVE ( 'NONE', #23623, #65100, #49237, .T. ) ;
#128079=DIRECTION ( 'NONE',  ( 0.7071067811865487940, 0.7071067811865463515, -0.000000000000000000 ) ) ;
#128080=AXIS2_PLACEMENT_3D ( 'NONE', #30907, #141810, #119996 ) ;
#128081=CARTESIAN_POINT ( 'NONE',  ( 3.469446951953614189E-15, 13.55218569542902785, 5.000000000000000000 ) ) ;
#128083=LINE ( 'NONE', #38210, #91869 ) ;
#128084=ORIENTED_EDGE ( 'NONE', *, *, #142555, .F. ) ;
#128085=CARTESIAN_POINT ( 'NONE',  ( 0.005480084712502889671, 28.92564299267938210, 4.000000000000000000 ) ) ;
#128086=LINE ( 'NONE', #49819, #16386 ) ;
#128087=CARTESIAN_POINT ( 'NONE',  ( 32.99451991528749062, 28.92564299267960948, 4.000000000000000000 ) ) ;
#128088=ADVANCED_FACE ( 'NONE', ( #14442 ), #92693, .F. ) ;
#128089=CARTESIAN_POINT ( 'NONE',  ( -14.60438740478481989, -0.8081507193758268315, 4.000000000000000000 ) ) ;
#128091=DIRECTION ( 'NONE',  ( -0.7071067811865486830, -0.7071067811865464625, 0.000000000000000000 ) ) ;
#128092=CARTESIAN_POINT ( 'NONE',  ( 17.52487387214943837, 14.25929247661557220, 9.797011795316677762 ) ) ;
#128094=PLANE ( 'NONE',  #139617 ) ;
#128096=ORIENTED_EDGE ( 'NONE', *, *, #44082, .T. ) ;
#128097=ORIENTED_EDGE ( 'NONE', *, *, #99940, .F. ) ;
#128100=ORIENTED_EDGE ( 'NONE', *, *, #6508, .T. ) ;
#128101=FACE_OUTER_BOUND ( 'NONE', #52763, .T. ) ;
#128102=PLANE ( 'NONE',  #115119 ) ;
#128103=LINE ( 'NONE', #116492, #24905 ) ;
#128104=ORIENTED_EDGE ( 'NONE', *, *, #63844, .T. ) ;
#128105=CARTESIAN_POINT ( 'NONE',  ( -3.524001385854469870, 22.03583458319438648, 4.979811245910087614 ) ) ;
#128106=LINE ( 'NONE', #38937, #35167 ) ;
#128108=ORIENTED_EDGE ( 'NONE', *, *, #112248, .T. ) ;
#128109=DIRECTION ( 'NONE',  ( -0.7071067811865487940, 0.7071067811865463515, 0.000000000000000000 ) ) ;
#128110=DIRECTION ( 'NONE',  ( 1.000000000000000000, 0.000000000000000000, 0.000000000000000000 ) ) ;
#128112=ORIENTED_EDGE ( 'NONE', *, *, #79705, .F. ) ;
#128113=VECTOR ( 'NONE', #67028, 1000.000000000000000 ) ;
#128114=ORIENTED_EDGE ( 'NONE', *, *, #34040, .T. ) ;
#128115=LINE ( 'NONE', #62142, #101037 ) ;
#128116=CARTESIAN_POINT ( 'NONE',  ( 11.99999999999993072, 11.58746187583912324, 4.000000000000000000 ) ) ;
#128117=CARTESIAN_POINT ( 'NONE',  ( 2.292893218813443657, -9.740707523384184441, 5.000000000000000000 ) ) ;
#128118=LINE ( 'NONE', #117195, #23201 ) ;
#128121=DIRECTION ( 'NONE',  ( -0.7071067811865487940, 0.7071067811865463515, -0.000000000000000000 ) ) ;
#128122=ORIENTED_EDGE ( 'NONE', *, *, #11254, .T. ) ;
#128123=EDGE_CURVE ( 'NONE', #94183, #9187, #68846, .T. ) ;
#128125=AXIS2_PLACEMENT_3D ( 'NONE', #7596, #51137, #140968 ) ;
#128127=ORIENTED_EDGE ( 'NONE', *, *, #49823, .T. ) ;
#128128=EDGE_CURVE ( 'NONE', #5353, #27958, #103561, .T. ) ;
#128129=ORIENTED_EDGE ( 'NONE', *, *, #88668, .T. ) ;
#128130=ADVANCED_FACE ( 'NONE', ( #125347 ), #134088, .F. ) ;
#128131=VECTOR ( 'NONE', #112902, 1000.000000000000000 ) ;
#128135=ORIENTED_EDGE ( 'NONE', *, *, #77838, .T. ) ;
#128137=PLANE ( 'NONE',  #130549 ) ;
#128138=CARTESIAN_POINT ( 'NONE',  ( -5.510786437626906675, -27.52281430457051314, 5.000000000000000000 ) ) ;
#128139=DIRECTION ( 'NONE',  ( -0.7071067811865487940, 0.7071067811865463515, -0.000000000000000000 ) ) ;
#128141=PLANE ( 'NONE',  #86184 ) ;
#128142=ORIENTED_EDGE ( 'NONE', *, *, #88746, .F. ) ;
#128143=DIRECTION ( 'NONE',  ( 0.7071067811865487940, 0.7071067811865463515, -0.000000000000000000 ) ) ;
#128144=CARTESIAN_POINT ( 'NONE',  ( 11.99999999999991651, -18.03360074219755660, 5.000000000000000000 ) ) ;
#128145=ADVANCED_FACE ( 'NONE', ( #127476 ), #94820, .T. ) ;
#128147=DIRECTION ( 'NONE',  ( 0.3543493200069162685, -0.000000000000000000, -0.9351131265310288487 ) ) ;
#128148=ORIENTED_EDGE ( 'NONE', *, *, #89811, .F. ) ;
#128149=ADVANCED_FACE ( 'NONE', ( #27429 ), #40494, .F. ) ;
#128151=VERTEX_POINT ( 'NONE', #5673 ) ;
#128152=EDGE_LOOP ( 'NONE', ( #52658, #116386, #24020, #32595, #92933, #50901 ) ) ;
#128155=ORIENTED_EDGE ( 'NONE', *, *, #82645, .T. ) ;
#128156=EDGE_CURVE ( 'NONE', #75329, #94548, #52067, .T. ) ;
#128157=LINE ( 'NONE', #73755, #81351 ) ;
#128158=AXIS2_PLACEMENT_3D ( 'NONE', #65046, #118686, #63631 ) ;
#128159=FACE_OUTER_BOUND ( 'NONE', #24319, .T. ) ;
#128161=LINE ( 'NONE', #104213, #72621 ) ;
#128162=LINE ( 'NONE', #17237, #32845 ) ;
#128163=CARTESIAN_POINT ( 'NONE',  ( -12.48921356237309155, -27.52281430457064104, 5.000000000000000000 ) ) ;
#128164=ADVANCED_FACE ( 'NONE', ( #28889 ), #106397, .T. ) ;
#128165=DIRECTION ( 'NONE',  ( 0.6830127018922181881, 0.6830127018922202975, -0.2588190451025214056 ) ) ;
#128166=DIRECTION ( 'NONE',  ( 0.000000000000000000, 0.000000000000000000, -1.000000000000000000 ) ) ;
#128167=VECTOR ( 'NONE', #139740, 1000.000000000000000 ) ;
#128168=CARTESIAN_POINT ( 'NONE',  ( -33.48921356237309510, -27.52281430457078670, 5.000000000000000000 ) ) ;
#128169=CARTESIAN_POINT ( 'NONE',  ( 21.48921356237309155, -27.52281430457070499, 5.000000000000000000 ) ) ;
#128170=EDGE_LOOP ( 'NONE', ( #131585, #122466, #107435, #63409 ) ) ;
#128171=LINE ( 'NONE', #84653, #64541 ) ;
#128172=DIRECTION ( 'NONE',  ( -0.6830127018922180770, -0.6830127018922204085, -0.2588190451025213501 ) ) ;
#128173=ORIENTED_EDGE ( 'NONE', *, *, #84284, .F. ) ;
#128174=VERTEX_POINT ( 'NONE', #16555 ) ;
#128176=LINE ( 'NONE', #108751, #132050 ) ;
#128178=VERTEX_POINT ( 'NONE', #6357 ) ;
#128179=LINE ( 'NONE', #97665, #26067 ) ;
#128180=DIRECTION ( 'NONE',  ( 0.6830127018922180770, -0.6830127018922204085, -0.2588190451025213501 ) ) ;
#128181=CARTESIAN_POINT ( 'NONE',  ( 2.292893218813443657, -18.74070752338408852, 5.000000000000000000 ) ) ;
#128183=ORIENTED_EDGE ( 'NONE', *, *, #101514, .F. ) ;
#128185=ORIENTED_EDGE ( 'NONE', *, *, #120630, .T. ) ;
#128186=AXIS2_PLACEMENT_3D ( 'NONE', #96523, #5943, #29860 ) ;
#128187=EDGE_CURVE ( 'NONE', #100848, #123054, #116603, .T. ) ;
#128190=FACE_OUTER_BOUND ( 'NONE', #134936, .T. ) ;
#128193=ORIENTED_EDGE ( 'NONE', *, *, #19445, .T. ) ;
#128194=ORIENTED_EDGE ( 'NONE', *, *, #40625, .F. ) ;
#128195=LINE ( 'NONE', #141177, #42673 ) ;
#128196=DIRECTION ( 'NONE',  ( -0.7071067811865486830, 0.7071067811865464625, 0.000000000000000000 ) ) ;
#128197=DIRECTION ( 'NONE',  ( -0.7071067811865486830, -0.7071067811865464625, 0.000000000000000000 ) ) ;
#128199=FACE_OUTER_BOUND ( 'NONE', #42584, .T. ) ;
#128200=CARTESIAN_POINT ( 'NONE',  ( -26.99999999999981171, 4.965500833774304290, -4.007596771432594629 ) ) ;
#128201=CARTESIAN_POINT ( 'NONE',  ( -5.381615093979999820, -2.240707523384260824, 13.37739548510240617 ) ) ;
#128202=VECTOR ( 'NONE', #11705, 1000.000000000000000 ) ;
#128203=EDGE_CURVE ( 'NONE', #57963, #16196, #105695, .T. ) ;
#128204=DIRECTION ( 'NONE',  ( 0.7071067811865486830, -0.7071067811865464625, -0.000000000000000000 ) ) ;
#128205=ORIENTED_EDGE ( 'NONE', *, *, #19289, .T. ) ;
#128206=PLANE ( 'NONE',  #90419 ) ;
#128211=DIRECTION ( 'NONE',  ( -0.7071067811865486830, 0.7071067811865464625, 0.000000000000000000 ) ) ;
#128213=EDGE_CURVE ( 'NONE', #77481, #19566, #62241, .T. ) ;
#128214=LINE ( 'NONE', #106399, #74671 ) ;
#128215=CARTESIAN_POINT ( 'NONE',  ( 34.92499999999998295, -9.908632306349565155, -7.176634499130175371 ) ) ;
#128216=ORIENTED_EDGE ( 'NONE', *, *, #139385, .F. ) ;
#128218=VERTEX_POINT ( 'NONE', #95556 ) ;
#128220=DIRECTION ( 'NONE',  ( -0.7071067811865486830, -0.7071067811865464625, -0.000000000000000000 ) ) ;
#128222=LINE ( 'NONE', #131065, #99381 ) ;
#128223=VECTOR ( 'NONE', #20253, 1000.000000000000000 ) ;
#128224=LINE ( 'NONE', #49952, #138563 ) ;
#128225=CARTESIAN_POINT ( 'NONE',  ( 9.489213562373095101, -27.52281430457062328, 5.000000000000000000 ) ) ;
#128226=LINE ( 'NONE', #28190, #123550 ) ;
#128227=CARTESIAN_POINT ( 'NONE',  ( -18.29974487139159223, -27.71228299555219010, 4.000000000000000000 ) ) ;
#128230=VECTOR ( 'NONE', #15648, 1000.000000000000227 ) ;
#128232=CARTESIAN_POINT ( 'NONE',  ( -17.99451991528748351, 28.92564299267950645, 4.000000000000000000 ) ) ;
#128233=CARTESIAN_POINT ( 'NONE',  ( -9.792893218813384593, -8.240707523384198652, 5.000000000000000000 ) ) ;
#128234=VERTEX_POINT ( 'NONE', #139818 ) ;
#128235=EDGE_LOOP ( 'NONE', ( #23355, #97450, #86395, #71245 ) ) ;
#128237=DIRECTION ( 'NONE',  ( -0.7071067811865486830, -0.7071067811865464625, 0.000000000000000000 ) ) ;
#128238=ORIENTED_EDGE ( 'NONE', *, *, #132187, .T. ) ;
#128239=ADVANCED_FACE ( 'NONE', ( #73817 ), #54931, .F. ) ;
#128240=CARTESIAN_POINT ( 'NONE',  ( 8.207106781186489286, -2.240707523384260824, 5.000000000000000000 ) ) ;
#128241=DIRECTION ( 'NONE',  ( 0.7071067811865487940, 0.7071067811865463515, 0.000000000000000000 ) ) ;
#128242=VECTOR ( 'NONE', #18473, 1000.000000000000000 ) ;
#128245=DIRECTION ( 'NONE',  ( 0.7071067811865487940, 0.7071067811865463515, 0.000000000000000000 ) ) ;
#128246=LINE ( 'NONE', #16599, #92714 ) ;
#128247=CARTESIAN_POINT ( 'NONE',  ( -16.17183060077636014, -8.240707523384191546, 4.000000000000000000 ) ) ;
#128248=LINE ( 'NONE', #72474, #141499 ) ;
#128249=ADVANCED_FACE ( 'NONE', ( #99847 ), #66519, .T. ) ;
#128250=ADVANCED_FACE ( 'NONE', ( #20122 ), #9217, .F. ) ;
#128251=DIRECTION ( 'NONE',  ( -0.7071067811865486830, -0.7071067811865464625, 0.000000000000000000 ) ) ;
#128252=LINE ( 'NONE', #105736, #3444 ) ;
#128253=DIRECTION ( 'NONE',  ( 0.6830127018922180770, -0.6830127018922204085, -0.2588190451025213501 ) ) ;
#128254=LINE ( 'NONE', #48543, #103151 ) ;
#128255=DIRECTION ( 'NONE',  ( -0.000000000000000000, 0.000000000000000000, 1.000000000000000000 ) ) ;
#128256=PLANE ( 'NONE',  #84948 ) ;
#128257=CARTESIAN_POINT ( 'NONE',  ( 7.499999999999951150, 9.052185695429074030, 5.000000000000000000 ) ) ;
#128258=CARTESIAN_POINT ( 'NONE',  ( 13.49999999999990052, -15.29013452822853480, 0.3645803511610678505 ) ) ;
#128259=ORIENTED_EDGE ( 'NONE', *, *, #102383, .T. ) ;
#128263=VERTEX_POINT ( 'NONE', #31738 ) ;
#128265=LINE ( 'NONE', #63025, #57339 ) ;
#128266=ORIENTED_EDGE ( 'NONE', *, *, #132645, .T. ) ;
#128268=CARTESIAN_POINT ( 'NONE',  ( -24.79289321881328334, 9.759292476615614831, 5.000000000000000000 ) ) ;
#128269=PLANE ( 'NONE',  #37320 ) ;
#128272=EDGE_LOOP ( 'NONE', ( #128468, #128509, #48581, #46957 ) ) ;
#128273=DIRECTION ( 'NONE',  ( 0.000000000000000000, 0.000000000000000000, 1.000000000000000000 ) ) ;
#128274=VERTEX_POINT ( 'NONE', #98424 ) ;
#128275=CARTESIAN_POINT ( 'NONE',  ( 24.06011071044004979, -9.740707523384187994, 10.89222023123375216 ) ) ;
#128276=DIRECTION ( 'NONE',  ( -0.7071067811865487940, 0.7071067811865463515, -0.000000000000000000 ) ) ;
#128277=DIRECTION ( 'NONE',  ( 0.7071067811865486830, -0.7071067811865464625, -0.000000000000000000 ) ) ;
#128278=ORIENTED_EDGE ( 'NONE', *, *, #31528, .F. ) ;
#128279=ORIENTED_EDGE ( 'NONE', *, *, #42057, .T. ) ;
#128281=DIRECTION ( 'NONE',  ( -0.000000000000000000, -0.3543493200069152693, 0.9351131265310292928 ) ) ;
#128282=CARTESIAN_POINT ( 'NONE',  ( -18.48921356237309510, -27.52281430457068367, 5.000000000000000000 ) ) ;
#128284=VECTOR ( 'NONE', #35817, 1000.000000000000000 ) ;
#128288=VECTOR ( 'NONE', #20859, 1000.000000000000000 ) ;
#128291=VERTEX_POINT ( 'NONE', #41914 ) ;
#128292=EDGE_CURVE ( 'NONE', #130094, #126512, #22960, .T. ) ;
#128293=FACE_OUTER_BOUND ( 'NONE', #142805, .T. ) ;
#128294=EDGE_LOOP ( 'NONE', ( #110221, #43393, #5568, #20318 ) ) ;
#128295=VERTEX_POINT ( 'NONE', #86123 ) ;
#128296=ADVANCED_FACE ( 'NONE', ( #109999 ), #22255, .F. ) ;
#128297=ADVANCED_FACE ( 'NONE', ( #31042 ), #64368, .F. ) ;
#128299=DIRECTION ( 'NONE',  ( 0.7071067811865487940, 0.7071067811865463515, 0.000000000000000000 ) ) ;
#128301=VERTEX_POINT ( 'NONE', #20845 ) ;
#128302=AXIS2_PLACEMENT_3D ( 'NONE', #57075, #32444, #21566 ) ;
#128303=LINE ( 'NONE', #48587, #133975 ) ;
#128305=DIRECTION ( 'NONE',  ( 0.7071067811865486830, -0.7071067811865464625, -0.000000000000000000 ) ) ;
#128306=LINE ( 'NONE', #42012, #73853 ) ;
#128307=DIRECTION ( 'NONE',  ( -0.000000000000000000, 0.3543493200069153248, 0.9351131265310292928 ) ) ;
#128308=ORIENTED_EDGE ( 'NONE', *, *, #138082, .F. ) ;
#128309=AXIS2_PLACEMENT_3D ( 'NONE', #19063, #106771, #32823 ) ;
#128310=DIRECTION ( 'NONE',  ( 0.000000000000000000, 0.3543493200069153248, 0.9351131265310291818 ) ) ;
#128311=DIRECTION ( 'NONE',  ( 0.7071067811865486830, -0.7071067811865464625, -0.000000000000000000 ) ) ;
#128312=ADVANCED_FACE ( 'NONE', ( #110685 ), #87547, .F. ) ;
#128313=VECTOR ( 'NONE', #20446, 1000.000000000000000 ) ;
#128314=VERTEX_POINT ( 'NONE', #133218 ) ;
#128315=CARTESIAN_POINT ( 'NONE',  ( -11.99999999999991296, 14.87792677143807651, -11.06722581663442639 ) ) ;
#128316=CARTESIAN_POINT ( 'NONE',  ( 0.000000000000000000, 0.000000000000000000, 5.000000000000000000 ) ) ;
#128317=DIRECTION ( 'NONE',  ( -0.7071067811865487940, 0.7071067811865463515, -0.000000000000000000 ) ) ;
#128318=EDGE_CURVE ( 'NONE', #122297, #28555, #21582, .T. ) ;
#128319=ORIENTED_EDGE ( 'NONE', *, *, #73298, .T. ) ;
#128320=CARTESIAN_POINT ( 'NONE',  ( 26.99999999999981171, 7.588810512006234354, -3.013526669885291387 ) ) ;
#128321=ORIENTED_EDGE ( 'NONE', *, *, #121701, .F. ) ;
#128323=ORIENTED_EDGE ( 'NONE', *, *, #90452, .T. ) ;
#128325=VECTOR ( 'NONE', #72041, 1000.000000000000000 ) ;
#128326=EDGE_CURVE ( 'NONE', #71954, #131551, #115160, .T. ) ;
#128327=DIRECTION ( 'NONE',  ( -0.7071067811865486830, 0.7071067811865464625, 0.000000000000000000 ) ) ;
#128328=LINE ( 'NONE', #63085, #14785 ) ;
#128330=DIRECTION ( 'NONE',  ( 1.000000000000000000, 0.000000000000000000, 0.000000000000000000 ) ) ;
#128331=DIRECTION ( 'NONE',  ( 0.3543493200069162685, -0.000000000000000000, -0.9351131265310288487 ) ) ;
#128332=FACE_OUTER_BOUND ( 'NONE', #120280, .T. ) ;
#128333=CARTESIAN_POINT ( 'NONE',  ( 51.48921356237309510, -27.52281430457091460, 5.000000000000000000 ) ) ;
#128335=CARTESIAN_POINT ( 'NONE',  ( -23.90332935812580928, -2.240707523384260824, 15.26439735382746932 ) ) ;
#128336=DIRECTION ( 'NONE',  ( -0.7071067811865487940, 0.7071067811865463515, 0.000000000000000000 ) ) ;
#128337=DIRECTION ( 'NONE',  ( -0.7071067811865486830, 0.7071067811865464625, 0.000000000000000000 ) ) ;
#128338=PLANE ( 'NONE',  #109622 ) ;
#128339=ORIENTED_EDGE ( 'NONE', *, *, #116326, .F. ) ;
#128340=ORIENTED_EDGE ( 'NONE', *, *, #80829, .F. ) ;
#128341=EDGE_CURVE ( 'NONE', #19533, #75064, #125373, .T. ) ;
#128343=ORIENTED_EDGE ( 'NONE', *, *, #85443, .T. ) ;
#128344=DIRECTION ( 'NONE',  ( -0.000000000000000000, -0.000000000000000000, 1.000000000000000000 ) ) ;
#128346=ORIENTED_EDGE ( 'NONE', *, *, #49779, .F. ) ;
#128347=CARTESIAN_POINT ( 'NONE',  ( 0.2997448713915885632, -27.71228299555206220, 4.000000000000000000 ) ) ;
#128348=PLANE ( 'NONE',  #131330 ) ;
#128349=CARTESIAN_POINT ( 'NONE',  ( 54.18398860626899705, 28.73617430169825226, 5.000000000000000000 ) ) ;
#128350=EDGE_CURVE ( 'NONE', #87398, #83942, #123766, .T. ) ;
#128351=ORIENTED_EDGE ( 'NONE', *, *, #104908, .T. ) ;
#128352=EDGE_CURVE ( 'NONE', #9752, #116419, #115923, .T. ) ;
#128353=LINE ( 'NONE', #105838, #64923 ) ;
#128354=VERTEX_POINT ( 'NONE', #112854 ) ;
#128355=DIRECTION ( 'NONE',  ( -0.7071067811865486830, -0.7071067811865464625, -0.000000000000000000 ) ) ;
#128356=EDGE_CURVE ( 'NONE', #103836, #75802, #14263, .T. ) ;
#128357=CARTESIAN_POINT ( 'NONE',  ( -41.99451991528749062, 28.92564299267967343, 4.000000000000000000 ) ) ;
#128361=DIRECTION ( 'NONE',  ( -0.7071067811865487940, 0.7071067811865463515, -0.000000000000000000 ) ) ;
#128362=CARTESIAN_POINT ( 'NONE',  ( 15.29974487139158867, -27.71228299555216879, 4.000000000000000000 ) ) ;
#128363=ORIENTED_EDGE ( 'NONE', *, *, #78359, .T. ) ;
#128364=VERTEX_POINT ( 'NONE', #125900 ) ;
#128365=CARTESIAN_POINT ( 'NONE',  ( 8.999999999999941380, -13.44781430457069149, 5.000000000000000000 ) ) ;
#128366=VERTEX_POINT ( 'NONE', #1219 ) ;
#128368=EDGE_CURVE ( 'NONE', #59884, #35253, #35339, .T. ) ;
#128369=PLANE ( 'NONE',  #7932 ) ;
#128371=VECTOR ( 'NONE', #87478, 1000.000000000000000 ) ;
#128372=ORIENTED_EDGE ( 'NONE', *, *, #120953, .T. ) ;
#128373=LINE ( 'NONE', #71143, #64424 ) ;
#128374=PLANE ( 'NONE',  #48870 ) ;
#128375=ORIENTED_EDGE ( 'NONE', *, *, #41035, .T. ) ;
#128376=CARTESIAN_POINT ( 'NONE',  ( 19.49999999999986500, -19.91253812416055879, 4.000000000000000000 ) ) ;
#128377=DIRECTION ( 'NONE',  ( -0.7071067811865487940, 0.7071067811865463515, 0.000000000000000000 ) ) ;
#128378=ORIENTED_EDGE ( 'NONE', *, *, #9227, .F. ) ;
#128379=DIRECTION ( 'NONE',  ( -0.7071067811865486830, 0.7071067811865464625, 0.000000000000000000 ) ) ;
#128380=ORIENTED_EDGE ( 'NONE', *, *, #57651, .T. ) ;
#128381=ORIENTED_EDGE ( 'NONE', *, *, #17630, .T. ) ;
#128382=CARTESIAN_POINT ( 'NONE',  ( 30.29974487139158867, -27.71228299555227537, 4.000000000000000000 ) ) ;
#128383=DIRECTION ( 'NONE',  ( -0.000000000000000000, -0.3543493200069152693, 0.9351131265310292928 ) ) ;
#128384=VECTOR ( 'NONE', #10962, 1000.000000000000000 ) ;
#128385=VERTEX_POINT ( 'NONE', #2655 ) ;
#128386=LINE ( 'NONE', #37821, #53451 ) ;
#128387=DIRECTION ( 'NONE',  ( -0.7071067811865487940, 0.7071067811865463515, -0.000000000000000000 ) ) ;
#128388=VECTOR ( 'NONE', #94346, 1000.000000000000227 ) ;
#128389=CARTESIAN_POINT ( 'NONE',  ( 45.48921356237309510, -27.52281430457087197, 5.000000000000000000 ) ) ;
#128390=DIRECTION ( 'NONE',  ( 0.7071067811865487940, -0.7071067811865463515, 0.000000000000000000 ) ) ;
#128391=VECTOR ( 'NONE', #17649, 1000.000000000000000 ) ;
#128392=LINE ( 'NONE', #7284, #18806 ) ;
#128394=LINE ( 'NONE', #94317, #90681 ) ;
#128395=EDGE_CURVE ( 'NONE', #68456, #98878, #91816, .T. ) ;
#128397=CARTESIAN_POINT ( 'NONE',  ( -22.00193056682082471, -22.22500000000000142, 4.500000000000000888 ) ) ;
#128398=DIRECTION ( 'NONE',  ( -0.7071067811865486830, -0.7071067811865464625, 0.000000000000000000 ) ) ;
#128399=CARTESIAN_POINT ( 'NONE',  ( 21.70710678118639336, 17.25929247661554200, 5.000000000000000000 ) ) ;
#128400=PLANE ( 'NONE',  #32714 ) ;
#128403=EDGE_LOOP ( 'NONE', ( #117289, #115187, #48522, #53630 ) ) ;
#128404=ORIENTED_EDGE ( 'NONE', *, *, #48196, .F. ) ;
#128406=VERTEX_POINT ( 'NONE', #14961 ) ;
#128408=EDGE_LOOP ( 'NONE', ( #34134, #30699, #138709, #142913 ) ) ;
#128410=CARTESIAN_POINT ( 'NONE',  ( -9.299744871391588674, -27.71228299555212971, 4.000000000000000000 ) ) ;
#128411=FACE_OUTER_BOUND ( 'NONE', #136429, .T. ) ;
#128412=ORIENTED_EDGE ( 'NONE', *, *, #14768, .T. ) ;
#128413=FACE_OUTER_BOUND ( 'NONE', #41864, .T. ) ;
#128414=CARTESIAN_POINT ( 'NONE',  ( 0.3281693992235271695, 8.259292476615637923, 4.000000000000000000 ) ) ;
#128415=CARTESIAN_POINT ( 'NONE',  ( 34.49999999999976552, 6.431123077392124188, 4.000000000000000000 ) ) ;
#128416=DIRECTION ( 'NONE',  ( 0.000000000000000000, 1.000000000000000000, -0.000000000000000000 ) ) ;
#128418=EDGE_CURVE ( 'NONE', #14590, #137119, #13525, .T. ) ;
#128419=ORIENTED_EDGE ( 'NONE', *, *, #62139, .F. ) ;
#128420=PLANE ( 'NONE',  #127468 ) ;
#128422=EDGE_CURVE ( 'NONE', #49880, #79180, #91142, .T. ) ;
#128423=DIRECTION ( 'NONE',  ( -0.7071067811865487940, 0.7071067811865463515, 0.000000000000000000 ) ) ;
#128424=PLANE ( 'NONE',  #1168 ) ;
#128425=CARTESIAN_POINT ( 'NONE',  ( -65.99451991528749772, 28.92564299267984396, 4.000000000000000000 ) ) ;
#128426=CARTESIAN_POINT ( 'NONE',  ( -2.999999999999973355, -9.412538124160660047, 4.000000000000000000 ) ) ;
#128427=VECTOR ( 'NONE', #67951, 1000.000000000000227 ) ;
#128429=CARTESIAN_POINT ( 'NONE',  ( 45.18398860626900415, 28.73617430169818832, 5.000000000000000000 ) ) ;
#128430=AXIS2_PLACEMENT_3D ( 'NONE', #57409, #2252, #71859 ) ;
#128431=DIRECTION ( 'NONE',  ( 0.6830127018922181881, 0.6830127018922202975, -0.2588190451025214056 ) ) ;
#128432=ORIENTED_EDGE ( 'NONE', *, *, #79206, .T. ) ;
#128433=ORIENTED_EDGE ( 'NONE', *, *, #15007, .T. ) ;
#128436=ORIENTED_EDGE ( 'NONE', *, *, #99080, .F. ) ;
#128438=EDGE_CURVE ( 'NONE', #84400, #8423, #4039, .T. ) ;
#128439=DIRECTION ( 'NONE',  ( -0.7071067811865487940, 0.7071067811865463515, -0.000000000000000000 ) ) ;
#128440=DIRECTION ( 'NONE',  ( 0.3543493200069162685, -0.000000000000000000, -0.9351131265310288487 ) ) ;
#128441=PLANE ( 'NONE',  #68823 ) ;
#128442=DIRECTION ( 'NONE',  ( -0.6830127018922181881, 0.6830127018922202975, -0.2588190451025214056 ) ) ;
#128443=EDGE_CURVE ( 'NONE', #77659, #28316, #46952, .T. ) ;
#128445=DIRECTION ( 'NONE',  ( 0.7071067811865487940, 0.7071067811865463515, 0.000000000000000000 ) ) ;
#128447=ORIENTED_EDGE ( 'NONE', *, *, #14636, .T. ) ;
#128448=CARTESIAN_POINT ( 'NONE',  ( -6.489213562373093325, -27.52281430457059841, 5.000000000000000000 ) ) ;
#128449=ORIENTED_EDGE ( 'NONE', *, *, #40741, .F. ) ;
#128450=EDGE_CURVE ( 'NONE', #85002, #78692, #41101, .T. ) ;
#128451=DIRECTION ( 'NONE',  ( 0.7071067811865486830, -0.7071067811865464625, -0.000000000000000000 ) ) ;
#128452=DIRECTION ( 'NONE',  ( 0.7071067811865487940, 0.7071067811865463515, 0.000000000000000000 ) ) ;
#128453=FACE_OUTER_BOUND ( 'NONE', #40688, .T. ) ;
#128456=ORIENTED_EDGE ( 'NONE', *, *, #47739, .T. ) ;
#128457=DIRECTION ( 'NONE',  ( -0.000000000000000000, -0.3543493200069152693, 0.9351131265310292928 ) ) ;
#128458=FACE_OUTER_BOUND ( 'NONE', #53723, .T. ) ;
#128459=CARTESIAN_POINT ( 'NONE',  ( 11.21837311707497342, 21.74787736706806740, 4.999607392498049308 ) ) ;
#128460=ADVANCED_FACE ( 'NONE', ( #89681 ), #113566, .T. ) ;
#128463=ORIENTED_EDGE ( 'NONE', *, *, #12524, .T. ) ;
#128464=PLANE ( 'NONE',  #62782 ) ;
#128465=EDGE_CURVE ( 'NONE', #123393, #69699, #23714, .T. ) ;
#128467=ORIENTED_EDGE ( 'NONE', *, *, #132696, .T. ) ;
#128468=ORIENTED_EDGE ( 'NONE', *, *, #101794, .T. ) ;
#128469=ORIENTED_EDGE ( 'NONE', *, *, #5304, .T. ) ;
#128470=VECTOR ( 'NONE', #13103, 1000.000000000000227 ) ;
#128471=EDGE_CURVE ( 'NONE', #5899, #27583, #16377, .T. ) ;
#128472=EDGE_CURVE ( 'NONE', #64350, #83371, #51282, .T. ) ;
#128474=PRODUCT_DEFINITION_CONTEXT ( 'detailed design', #129112, 'design' ) ;
#128475=ORIENTED_EDGE ( 'NONE', *, *, #24868, .T. ) ;
#128477=EDGE_CURVE ( 'NONE', #89594, #12213, #51914, .T. ) ;
#128479=FACE_BOUND ( 'NONE', #71985, .T. ) ;
#128480=ADVANCED_FACE ( 'NONE', ( #15643 ), #83848, .F. ) ;
#128482=DIRECTION ( 'NONE',  ( 0.7071067811865487940, -0.7071067811865463515, 0.000000000000000000 ) ) ;
#128483=DIRECTION ( 'NONE',  ( -0.7071067811865486830, 0.7071067811865464625, 0.000000000000000000 ) ) ;
#128484=EDGE_CURVE ( 'NONE', #57093, #32412, #41019, .T. ) ;
#128485=VERTEX_POINT ( 'NONE', #49786 ) ;
#128488=ORIENTED_EDGE ( 'NONE', *, *, #48582, .F. ) ;
#128489=DIRECTION ( 'NONE',  ( 0.7071067811865487940, 0.7071067811865463515, 0.000000000000000000 ) ) ;
#128490=ORIENTED_EDGE ( 'NONE', *, *, #129966, .F. ) ;
#128493=ORIENTED_EDGE ( 'NONE', *, *, #61472, .T. ) ;
#128496=CARTESIAN_POINT ( 'NONE',  ( 42.48921356237308800, -27.52281430457085065, 5.000000000000000000 ) ) ;
#128497=AXIS2_PLACEMENT_3D ( 'NONE', #134306, #25514, #126272 ) ;
#128498=CARTESIAN_POINT ( 'NONE',  ( -27.48921356237309155, -27.52281430457074762, 5.000000000000000000 ) ) ;
#128500=DIRECTION ( 'NONE',  ( 0.7071067811865486830, -0.7071067811865464625, -0.000000000000000000 ) ) ;
#128501=EDGE_CURVE ( 'NONE', #73867, #68609, #18517, .T. ) ;
#128503=VECTOR ( 'NONE', #110870, 1000.000000000000000 ) ;
#128504=CARTESIAN_POINT ( 'NONE',  ( -12.79333936457838661, 21.75929247661549581, 4.998822639870701856 ) ) ;
#128505=CARTESIAN_POINT ( 'NONE',  ( 34.42499999999998295, -21.72500000000000142, 0.000000000000000000 ) ) ;
#128506=DIRECTION ( 'NONE',  ( -0.7071067811865487940, 0.7071067811865463515, -0.000000000000000000 ) ) ;
#128507=FACE_OUTER_BOUND ( 'NONE', #20987, .T. ) ;
#128508=EDGE_LOOP ( 'NONE', ( #39888, #40833, #40315, #78825 ) ) ;
#128509=ORIENTED_EDGE ( 'NONE', *, *, #114068, .T. ) ;
#128511=DIRECTION ( 'NONE',  ( 1.000000000000000000, 0.000000000000000000, 0.000000000000000000 ) ) ;
#128512=ORIENTED_EDGE ( 'NONE', *, *, #74069, .F. ) ;
#128513=VERTEX_POINT ( 'NONE', #126575 ) ;
#128514=ORIENTED_EDGE ( 'NONE', *, *, #64840, .T. ) ;
#128517=VERTEX_POINT ( 'NONE', #61394 ) ;
#128519=VECTOR ( 'NONE', #132733, 1000.000000000000227 ) ;
#128520=EDGE_CURVE ( 'NONE', #132519, #49642, #94662, .T. ) ;
#128521=CARTESIAN_POINT ( 'NONE',  ( -34.92500000000001137, 10.70193056682090749, 4.500000000000000888 ) ) ;
#128522=VECTOR ( 'NONE', #43123, 999.9999999999998863 ) ;
#128525=VECTOR ( 'NONE', #98386, 1000.000000000000000 ) ;
#128526=CARTESIAN_POINT ( 'NONE',  ( -2.999999999999975131, 1.552185695429149304, 5.000000000000000000 ) ) ;
#128527=ORIENTED_EDGE ( 'NONE', *, *, #82428, .F. ) ;
#128528=DIRECTION ( 'NONE',  ( 0.3543493200069162685, -0.000000000000000000, -0.9351131265310288487 ) ) ;
#128530=CARTESIAN_POINT ( 'NONE',  ( -17.99999999999986855, -10.44781430457071991, 5.000000000000000000 ) ) ;
#128531=PLANE ( 'NONE',  #91280 ) ;
#128532=CARTESIAN_POINT ( 'NONE',  ( -15.18398860626900237, 28.73617430169797871, 5.000000000000000000 ) ) ;
#128534=DIRECTION ( 'NONE',  ( 0.7071067811865486830, -0.7071067811865464625, -0.000000000000000000 ) ) ;
#128535=ORIENTED_EDGE ( 'NONE', *, *, #22109, .F. ) ;
#128536=FACE_OUTER_BOUND ( 'NONE', #37536, .T. ) ;
#128537=FACE_OUTER_BOUND ( 'NONE', #120932, .T. ) ;
#128538=ORIENTED_EDGE ( 'NONE', *, *, #130876, .F. ) ;
#128539=CARTESIAN_POINT ( 'NONE',  ( -9.489213562373095101, -27.52281430457062328, 5.000000000000000000 ) ) ;
#128540=CARTESIAN_POINT ( 'NONE',  ( -39.18398860626899705, 28.73617430169814568, 5.000000000000000000 ) ) ;
#128541=CARTESIAN_POINT ( 'NONE',  ( -23.48334561358938899, 22.22500000000000142, 4.500000000000000888 ) ) ;
#128542=ORIENTED_EDGE ( 'NONE', *, *, #33910, .F. ) ;
#128543=CARTESIAN_POINT ( 'NONE',  ( -3.489213562373097322, -27.52281430457057709, 5.000000000000000000 ) ) ;
#128544=DIRECTION ( 'NONE',  ( 0.6830127018922180770, -0.6830127018922204085, -0.2588190451025213501 ) ) ;
#128545=CARTESIAN_POINT ( 'NONE',  ( 11.50183651486036496, -17.24070752338410628, 8.407044977365197624 ) ) ;
#128546=LINE ( 'NONE', #29213, #21708 ) ;
#128547=CARTESIAN_POINT ( 'NONE',  ( 16.17183060077635304, -20.24070752338408141, 4.000000000000000000 ) ) ;
#128548=ORIENTED_EDGE ( 'NONE', *, *, #90615, .F. ) ;
#128549=ORIENTED_EDGE ( 'NONE', *, *, #61278, .T. ) ;
#128550=CARTESIAN_POINT ( 'NONE',  ( -39.18398860626899705, 28.73617430169814568, 5.000000000000000000 ) ) ;
#128551=LINE ( 'NONE', #116946, #110778 ) ;
#128553=DIRECTION ( 'NONE',  ( 0.6830127018922180770, -0.6830127018922204085, -0.2588190451025213501 ) ) ;
#128554=DIRECTION ( 'NONE',  ( 0.6830127018922180770, -0.6830127018922204085, -0.2588190451025213501 ) ) ;
#128555=CARTESIAN_POINT ( 'NONE',  ( 9.792893218813388145, 12.75929247661558996, 5.000000000000000000 ) ) ;
#128556=ORIENTED_EDGE ( 'NONE', *, *, #73034, .T. ) ;
#128559=DIRECTION ( 'NONE',  ( 0.7071067811865487940, 0.7071067811865463515, -0.000000000000000000 ) ) ;
#128562=CARTESIAN_POINT ( 'NONE',  ( -21.79333936457831911, 21.75929247661549226, 4.998822639870701856 ) ) ;
#128563=VERTEX_POINT ( 'NONE', #116441 ) ;
#128564=DIRECTION ( 'NONE',  ( -0.7071067811865487940, 0.7071067811865463515, -0.000000000000000000 ) ) ;
#128565=EDGE_LOOP ( 'NONE', ( #57492, #92979, #42049, #61080 ) ) ;
#128566=ORIENTED_EDGE ( 'NONE', *, *, #88573, .T. ) ;
#128567=DIRECTION ( 'NONE',  ( -0.000000000000000000, -0.3543493200069152693, 0.9351131265310292928 ) ) ;
#128569=LINE ( 'NONE', #27104, #58159 ) ;
#128570=EDGE_CURVE ( 'NONE', #9436, #34226, #128737, .T. ) ;
#128571=DIRECTION ( 'NONE',  ( 0.7071067811865487940, -0.7071067811865463515, 0.000000000000000000 ) ) ;
#128574=EDGE_CURVE ( 'NONE', #25072, #44387, #140191, .T. ) ;
#128575=EDGE_CURVE ( 'NONE', #1453, #98880, #28006, .T. ) ;
#128576=VERTEX_POINT ( 'NONE', #72976 ) ;
#128577=CARTESIAN_POINT ( 'NONE',  ( -32.99999999999975842, -16.06887692260765377, 4.000000000000000000 ) ) ;
#128579=FACE_OUTER_BOUND ( 'NONE', #122569, .T. ) ;
#128580=DIRECTION ( 'NONE',  ( 0.000000000000000000, 0.000000000000000000, -1.000000000000000000 ) ) ;
#128581=DIRECTION ( 'NONE',  ( 0.7071067811865486830, -0.7071067811865464625, -0.000000000000000000 ) ) ;
#128582=CARTESIAN_POINT ( 'NONE',  ( 45.29974487139158867, -27.71228299555237840, 4.000000000000000000 ) ) ;
#128583=EDGE_CURVE ( 'NONE', #50248, #135356, #17126, .T. ) ;
#128585=EDGE_CURVE ( 'NONE', #99872, #105758, #95392, .T. ) ;
#128586=AXIS2_PLACEMENT_3D ( 'NONE', #3921, #46082, #135917 ) ;
#128589=ORIENTED_EDGE ( 'NONE', *, *, #133885, .F. ) ;
#128591=DIRECTION ( 'NONE',  ( 0.3543493200069162685, -0.000000000000000000, -0.9351131265310288487 ) ) ;
#128593=ADVANCED_FACE ( 'NONE', ( #40335 ), #137488, .F. ) ;
#128594=DIRECTION ( 'NONE',  ( -0.7071067811865486830, -0.7071067811865464625, -0.000000000000000000 ) ) ;
#128595=DIRECTION ( 'NONE',  ( -0.6830127018922181881, 0.6830127018922202975, -0.2588190451025214056 ) ) ;
#128596=VERTEX_POINT ( 'NONE', #105540 ) ;
#128597=CARTESIAN_POINT ( 'NONE',  ( 0.000000000000000000, 0.000000000000000000, 5.000000000000000000 ) ) ;
#128598=ADVANCED_FACE ( 'NONE', ( #6199 ), #50476, .F. ) ;
#128601=ORIENTED_EDGE ( 'NONE', *, *, #37309, .F. ) ;
#128602=FACE_OUTER_BOUND ( 'NONE', #48095, .T. ) ;
#128605=FACE_OUTER_BOUND ( 'NONE', #46671, .T. ) ;
#128606=EDGE_CURVE ( 'NONE', #71584, #116900, #142489, .T. ) ;
#128608=PLANE ( 'NONE',  #76780 ) ;
#128609=DIRECTION ( 'NONE',  ( 0.7071067811865487940, -0.7071067811865463515, 0.000000000000000000 ) ) ;
#128610=DIRECTION ( 'NONE',  ( 0.000000000000000000, -1.000000000000000000, 0.000000000000000000 ) ) ;
#128611=CARTESIAN_POINT ( 'NONE',  ( -2.816011393730999401, 28.73617430169785436, 5.000000000000000000 ) ) ;
#128612=VERTEX_POINT ( 'NONE', #44638 ) ;
#128613=DIRECTION ( 'NONE',  ( -0.000000000000000000, 0.3543493200069153248, 0.9351131265310292928 ) ) ;
#128614=CARTESIAN_POINT ( 'NONE',  ( 59.99451991528749772, 28.92564299267980132, 4.000000000000000000 ) ) ;
#128615=DIRECTION ( 'NONE',  ( -0.7071067811865486830, -0.7071067811865464625, -0.000000000000000000 ) ) ;
#128616=ADVANCED_FACE ( 'NONE', ( #53310 ), #341, .F. ) ;
#128617=LINE ( 'NONE', #62655, #57941 ) ;
#128618=DIRECTION ( 'NONE',  ( 0.7071067811865486830, -0.7071067811865464625, -0.000000000000000000 ) ) ;
#128619=VECTOR ( 'NONE', #105054, 1000.000000000000000 ) ;
#128620=EDGE_LOOP ( 'NONE', ( #93263, #13756, #44605, #22358 ) ) ;
#128622=ORIENTED_EDGE ( 'NONE', *, *, #43553, .F. ) ;
#128623=AXIS2_PLACEMENT_3D ( 'NONE', #116554, #51311, #61501 ) ;
#128624=DIRECTION ( 'NONE',  ( 1.000000000000000000, 0.000000000000000000, 0.000000000000000000 ) ) ;
#128626=LINE ( 'NONE', #40904, #99693 ) ;
#128627=EDGE_CURVE ( 'NONE', #108744, #101850, #88828, .T. ) ;
#128628=CARTESIAN_POINT ( 'NONE',  ( 29.28769006033951783, -21.73547319004780931, 4.999917730833664642 ) ) ;
#128629=PLANE ( 'NONE',  #89480 ) ;
#128630=ORIENTED_EDGE ( 'NONE', *, *, #18015, .T. ) ;
#128631=VERTEX_POINT ( 'NONE', #54077 ) ;
#128634=ORIENTED_EDGE ( 'NONE', *, *, #141537, .T. ) ;
#128637=FACE_OUTER_BOUND ( 'NONE', #73292, .T. ) ;
#128638=ORIENTED_EDGE ( 'NONE', *, *, #26455, .T. ) ;
#128639=EDGE_CURVE ( 'NONE', #7557, #80484, #118568, .T. ) ;
#128640=CARTESIAN_POINT ( 'NONE',  ( -33.18398860626899705, 28.73617430169810305, 5.000000000000000000 ) ) ;
#128641=EDGE_CURVE ( 'NONE', #126683, #3334, #19268, .T. ) ;
#128642=FACE_BOUND ( 'NONE', #133323, .T. ) ;
#128645=DIRECTION ( 'NONE',  ( 0.7071067811865486830, -0.7071067811865464625, -0.000000000000000000 ) ) ;
#128646=CARTESIAN_POINT ( 'NONE',  ( -11.29289321881337571, -9.740707523384186217, 5.000000000000000000 ) ) ;
#128647=ORIENTED_EDGE ( 'NONE', *, *, #140104, .F. ) ;
#128650=ORIENTED_EDGE ( 'NONE', *, *, #19793, .T. ) ;
#128651=VERTEX_POINT ( 'NONE', #97529 ) ;
#128653=ORIENTED_EDGE ( 'NONE', *, *, #95673, .T. ) ;
#128654=CARTESIAN_POINT ( 'NONE',  ( 8.816011393731004731, 28.73617430169781173, 5.000000000000000000 ) ) ;
#128655=EDGE_CURVE ( 'NONE', #75592, #38197, #43177, .T. ) ;
#128656=DIRECTION ( 'NONE',  ( -0.3543493200069163240, 0.000000000000000000, -0.9351131265310288487 ) ) ;
#128657=DIRECTION ( 'NONE',  ( -0.7071067811865486830, -0.7071067811865464625, 0.000000000000000000 ) ) ;
#128658=CARTESIAN_POINT ( 'NONE',  ( 24.98480450340313652, 2.536990198832462351, 5.000000000000000000 ) ) ;
#128659=CARTESIAN_POINT ( 'NONE',  ( 6.328169399223492420, 5.259292476615662792, 4.000000000000000000 ) ) ;
#128660=ORIENTED_EDGE ( 'NONE', *, *, #27023, .T. ) ;
#128662=EDGE_CURVE ( 'NONE', #29861, #72725, #120702, .T. ) ;
#128663=CARTESIAN_POINT ( 'NONE',  ( -63.48921356237309510, -27.52281430457099631, 5.000000000000000000 ) ) ;
#128665=DIRECTION ( 'NONE',  ( 0.6830127018922180770, -0.6830127018922204085, -0.2588190451025213501 ) ) ;
#128666=CARTESIAN_POINT ( 'NONE',  ( 14.67183060077637080, -15.74070752338412049, 4.000000000000000000 ) ) ;
#128667=CARTESIAN_POINT ( 'NONE',  ( -45.48921356237309510, -27.52281430457087197, 5.000000000000000000 ) ) ;
#128668=CARTESIAN_POINT ( 'NONE',  ( -32.19990655525713663, -22.22500000000000142, 3.967360224444566708 ) ) ;
#128669=ORIENTED_EDGE ( 'NONE', *, *, #54619, .T. ) ;
#128670=CARTESIAN_POINT ( 'NONE',  ( 9.328169399223467551, 2.259292476615690770, 4.000000000000000000 ) ) ;
#128671=CARTESIAN_POINT ( 'NONE',  ( 34.92499999999998295, 22.22500000000000142, 4.000000000000000000 ) ) ;
#128672=EDGE_LOOP ( 'NONE', ( #46499, #54816, #141701, #15266 ) ) ;
#128673=ADVANCED_FACE ( 'NONE', ( #21416 ), #96778, .F. ) ;
#128674=ORIENTED_EDGE ( 'NONE', *, *, #142582, .F. ) ;
#128675=ORIENTED_EDGE ( 'NONE', *, *, #25315, .F. ) ;
#128676=ADVANCED_FACE ( 'NONE', ( #107689 ), #19964, .F. ) ;
#128678=ORIENTED_EDGE ( 'NONE', *, *, #75932, .T. ) ;
#128679=VECTOR ( 'NONE', #137731, 1000.000000000000000 ) ;
#128680=EDGE_CURVE ( 'NONE', #142920, #77362, #88099, .T. ) ;
#128683=ORIENTED_EDGE ( 'NONE', *, *, #116222, .F. ) ;
#128684=VECTOR ( 'NONE', #107569, 1000.000000000000000 ) ;
#128685=LINE ( 'NONE', #61336, #47145 ) ;
#128686=ORIENTED_EDGE ( 'NONE', *, *, #113138, .T. ) ;
#128687=DIRECTION ( 'NONE',  ( -0.7071067811865487940, 0.7071067811865463515, -0.000000000000000000 ) ) ;
#128688=CARTESIAN_POINT ( 'NONE',  ( -15.29974487139158867, -27.71228299555216879, 4.000000000000000000 ) ) ;
#128689=DIRECTION ( 'NONE',  ( 4.681814790819592407E-17, 0.3543493200069153248, 0.9351131265310292928 ) ) ;
#128690=VERTEX_POINT ( 'NONE', #98949 ) ;
#128691=VERTEX_POINT ( 'NONE', #141032 ) ;
#128692=DIRECTION ( 'NONE',  ( 0.3543493200069163240, 0.000000000000000000, -0.9351131265310288487 ) ) ;
#128696=ORIENTED_EDGE ( 'NONE', *, *, #117351, .T. ) ;
#128697=VERTEX_POINT ( 'NONE', #22102 ) ;
#128698=EDGE_LOOP ( 'NONE', ( #116507, #110891, #118074, #65097, #93021 ) ) ;
#128701=CARTESIAN_POINT ( 'NONE',  ( -20.54016161050247646, 18.75929247661552779, 8.305906642995438460 ) ) ;
#128703=CARTESIAN_POINT ( 'NONE',  ( -0.7928932188134485415, -14.24070752338414003, 5.000000000000000000 ) ) ;
#128704=DIRECTION ( 'NONE',  ( -0.000000000000000000, 0.3543493200069153248, 0.9351131265310292928 ) ) ;
#128705=EDGE_CURVE ( 'NONE', #15253, #50127, #86682, .T. ) ;
#128707=DIRECTION ( 'NONE',  ( 0.7071067811865487940, -0.7071067811865463515, 0.000000000000000000 ) ) ;
#128709=DIRECTION ( 'NONE',  ( -0.6830127018922181881, 0.6830127018922202975, -0.2588190451025214056 ) ) ;
#128711=DIRECTION ( 'NONE',  ( 0.6830127018922180770, -0.6830127018922204085, -0.2588190451025213501 ) ) ;
#128712=CARTESIAN_POINT ( 'NONE',  ( 24.79289321881327623, 18.75929247661552779, 5.000000000000000000 ) ) ;
#128713=VECTOR ( 'NONE', #104704, 999.9999999999998863 ) ;
#128714=ORIENTED_EDGE ( 'NONE', *, *, #140704, .T. ) ;
#128717=ORIENTED_EDGE ( 'NONE', *, *, #115524, .F. ) ;
#128718=AXIS2_PLACEMENT_3D ( 'NONE', #76921, #21064, #30543 ) ;
#128719=ORIENTED_EDGE ( 'NONE', *, *, #32490, .F. ) ;
#128720=EDGE_LOOP ( 'NONE', ( #97031, #6147, #29056, #2016 ) ) ;
#128721=FACE_OUTER_BOUND ( 'NONE', #141629, .T. ) ;
#128722=DIRECTION ( 'NONE',  ( -1.000000000000000000, 0.000000000000000000, 0.000000000000000000 ) ) ;
#128723=CARTESIAN_POINT ( 'NONE',  ( -17.18650864602350126, -15.74070752338412404, 8.904080028138981362 ) ) ;
#128724=VECTOR ( 'NONE', #11196, 1000.000000000000000 ) ;
#128726=CARTESIAN_POINT ( 'NONE',  ( 21.70701326429288613, -21.74070752338406365, 4.999753212805217117 ) ) ;
#128729=LINE ( 'NONE', #140322, #106336 ) ;
#128730=DIRECTION ( 'NONE',  ( 0.7071067811865487940, -0.7071067811865463515, 0.000000000000000000 ) ) ;
#128731=CARTESIAN_POINT ( 'NONE',  ( 6.489213562373093325, -27.52281430457059841, 5.000000000000000000 ) ) ;
#128732=CARTESIAN_POINT ( 'NONE',  ( 34.42499999999998295, 21.72500000000000142, 0.5000000000000000000 ) ) ;
#128734=FACE_OUTER_BOUND ( 'NONE', #91731, .T. ) ;
#128736=LINE ( 'NONE', #75106, #32294 ) ;
#128737=LINE ( 'NONE', #38879, #46469 ) ;
#128738=VERTEX_POINT ( 'NONE', #64209 ) ;
#128739=LINE ( 'NONE', #27270, #44022 ) ;
#128740=PLANE ( 'NONE',  #93550 ) ;
#128741=ADVANCED_FACE ( 'NONE', ( #20681 ), #64927, .F. ) ;
#128743=ORIENTED_EDGE ( 'NONE', *, *, #53272, .F. ) ;
#128744=LINE ( 'NONE', #96790, #132453 ) ;
#128745=DIRECTION ( 'NONE',  ( -0.7071067811865487940, 0.7071067811865463515, 0.000000000000000000 ) ) ;
#128746=EDGE_CURVE ( 'NONE', #58008, #61053, #131606, .T. ) ;
#128748=ADVANCED_FACE ( 'NONE', ( #12655 ), #59078, .F. ) ;
#128749=CARTESIAN_POINT ( 'NONE',  ( 75.48921356237309510, -27.52281430457107803, 5.000000000000000000 ) ) ;
#128750=PLANE ( 'NONE',  #52947 ) ;
#128751=ORIENTED_EDGE ( 'NONE', *, *, #86039, .T. ) ;
#128752=EDGE_CURVE ( 'NONE', #23590, #5533, #46042, .T. ) ;
#128753=CARTESIAN_POINT ( 'NONE',  ( 38.99451991528749062, 28.92564299267965211, 4.000000000000000000 ) ) ;
#128754=EDGE_CURVE ( 'NONE', #108299, #114924, #112003, .T. ) ;
#128755=CARTESIAN_POINT ( 'NONE',  ( 34.49999999999975842, 5.696342897626535340, -7.587980461218318595 ) ) ;
#128757=AXIS2_PLACEMENT_3D ( 'NONE', #104123, #6226, #113596 ) ;
#128758=FACE_OUTER_BOUND ( 'NONE', #140737, .T. ) ;
#128759=EDGE_CURVE ( 'NONE', #42096, #95953, #90225, .T. ) ;
#128760=VERTEX_POINT ( 'NONE', #34426 ) ;
#128761=CARTESIAN_POINT ( 'NONE',  ( 32.99999999999976552, 13.93112307739204248, 4.000000000000000000 ) ) ;
#128762=EDGE_CURVE ( 'NONE', #35471, #39260, #1051, .T. ) ;
#128765=DIRECTION ( 'NONE',  ( -0.3543493200069162685, -0.000000000000000000, -0.9351131265310288487 ) ) ;
#128766=VECTOR ( 'NONE', #19960, 1000.000000000000227 ) ;
#128767=DIRECTION ( 'NONE',  ( -0.000000000000000000, -0.3543493200069152693, 0.9351131265310292928 ) ) ;
#128768=ORIENTED_EDGE ( 'NONE', *, *, #33729, .T. ) ;
#128770=( BOUNDED_CURVE ( )  B_SPLINE_CURVE ( 3, ( #74942, #39452, #63363, #95226 ),
 .UNSPECIFIED., .F., .T. ) 
 B_SPLINE_CURVE_WITH_KNOTS ( ( 4, 4 ),
 ( 2.001653308786169205, 3.503810798801451742 ),
 .UNSPECIFIED. ) 
 CURVE ( )  GEOMETRIC_REPRESENTATION_ITEM ( )  RATIONAL_B_SPLINE_CURVE ( ( 1.000000000000000000, 0.8206354192515237234, 0.8206354192515237234, 1.000000000000000000 ) ) 
 REPRESENTATION_ITEM ( '' )  );
#128771=ADVANCED_FACE ( 'NONE', ( #3884 ), #123610, .F. ) ;
#128772=LINE ( 'NONE', #85254, #9447 ) ;
#128773=PLANE ( 'NONE',  #41574 ) ;
#128774=LINE ( 'NONE', #141068, #112439 ) ;
#128775=ORIENTED_EDGE ( 'NONE', *, *, #134738, .F. ) ;
#128777=CARTESIAN_POINT ( 'NONE',  ( 47.99451991528749062, 28.92564299267971251, 4.000000000000000000 ) ) ;
#128779=ADVANCED_FACE ( 'NONE', ( #91657 ), #33740, .F. ) ;
#128780=VERTEX_POINT ( 'NONE', #3205 ) ;
#128781=AXIS2_PLACEMENT_3D ( 'NONE', #118486, #85863, #54687 ) ;
#128782=ORIENTED_EDGE ( 'NONE', *, *, #119815, .F. ) ;
#128784=ORIENTED_EDGE ( 'NONE', *, *, #34344, .F. ) ;
#128786=CARTESIAN_POINT ( 'NONE',  ( -4.828169399223503078, 18.75929247661552424, 4.000000000000000000 ) ) ;
#128788=FACE_OUTER_BOUND ( 'NONE', #46489, .T. ) ;
#128789=ORIENTED_EDGE ( 'NONE', *, *, #51509, .T. ) ;
#128791=DIRECTION ( 'NONE',  ( -1.000000000000000000, 0.000000000000000000, -0.000000000000000000 ) ) ;
#128792=EDGE_LOOP ( 'NONE', ( #72689, #37771, #48351, #139623 ) ) ;
#128793=VECTOR ( 'NONE', #20044, 1000.000000000000114 ) ;
#128794=DIRECTION ( 'NONE',  ( -0.000000000000000000, 0.000000000000000000, 1.000000000000000000 ) ) ;
#128795=ADVANCED_FACE ( 'NONE', ( #101097 ), #114122, .F. ) ;
#128796=DIRECTION ( 'NONE',  ( 0.7071067811865486830, -0.7071067811865464625, -0.000000000000000000 ) ) ;
#128797=CARTESIAN_POINT ( 'NONE',  ( -57.48921356237308800, -27.52281430457095368, 5.000000000000000000 ) ) ;
#128798=EDGE_CURVE ( 'NONE', #92118, #92154, #100408, .T. ) ;
#128799=ORIENTED_EDGE ( 'NONE', *, *, #29895, .T. ) ;
#128800=EDGE_LOOP ( 'NONE', ( #90919, #33071, #42411, #108640 ) ) ;
#128801=VECTOR ( 'NONE', #133274, 1000.000000000000000 ) ;
#128803=CARTESIAN_POINT ( 'NONE',  ( 6.183988606268994381, 28.73617430169791476, 5.000000000000000000 ) ) ;
#128804=LINE ( 'NONE', #62870, #122990 ) ;
#128806=DIRECTION ( 'NONE',  ( 0.7071067811865487940, 0.7071067811865463515, 0.000000000000000000 ) ) ;
#128807=EDGE_CURVE ( 'NONE', #56699, #139467, #68511, .T. ) ;
#128808=VECTOR ( 'NONE', #91695, 1000.000000000000000 ) ;
#128809=VECTOR ( 'NONE', #61964, 999.9999999999998863 ) ;
#128810=CARTESIAN_POINT ( 'NONE',  ( -17.99999999999986500, -3.412538124160723108, 4.000000000000000000 ) ) ;
#128811=VERTEX_POINT ( 'NONE', #90970 ) ;
#128812=VECTOR ( 'NONE', #82625, 1000.000000000000000 ) ;
#128815=EDGE_CURVE ( 'NONE', #47195, #23039, #80104, .T. ) ;
#128816=ORIENTED_EDGE ( 'NONE', *, *, #132510, .F. ) ;
#128817=VECTOR ( 'NONE', #86148, 1000.000000000000000 ) ;
#128819=CARTESIAN_POINT ( 'NONE',  ( -31.49999999999978684, 1.030536316426473809, -5.498701923753729126 ) ) ;
#128820=CARTESIAN_POINT ( 'NONE',  ( 23.99999999999983302, -6.108550654416937675, -3.114665004254912439 ) ) ;
#128821=ORIENTED_EDGE ( 'NONE', *, *, #6380, .T. ) ;
#128822=DIRECTION ( 'NONE',  ( -0.7071067811865486830, -0.7071067811865464625, -0.000000000000000000 ) ) ;
#128823=LINE ( 'NONE', #85302, #21773 ) ;
#128824=CARTESIAN_POINT ( 'NONE',  ( 34.92499999999998295, -7.298069433178939747, 4.500000000000000888 ) ) ;
#128825=LINE ( 'NONE', #29502, #16063 ) ;
#128827=ORIENTED_EDGE ( 'NONE', *, *, #71929, .T. ) ;
#128828=CARTESIAN_POINT ( 'NONE',  ( 33.78162688292471216, 21.74787736706807095, 4.999607392498048419 ) ) ;
#128829=DIRECTION ( 'NONE',  ( -0.7071067811865486830, -0.7071067811865464625, 0.000000000000000000 ) ) ;
#128833=ORIENTED_EDGE ( 'NONE', *, *, #51044, .T. ) ;
#128834=ADVANCED_FACE ( 'NONE', ( #13358 ), #57631, .F. ) ;
#128835=DIRECTION ( 'NONE',  ( -0.000000000000000000, -0.000000000000000000, 1.000000000000000000 ) ) ;
#128836=VERTEX_POINT ( 'NONE', #14078 ) ;
#128837=EDGE_CURVE ( 'NONE', #1472, #102338, #25678, .T. ) ;
#128839=ORIENTED_EDGE ( 'NONE', *, *, #94425, .T. ) ;
#128840=ORIENTED_EDGE ( 'NONE', *, *, #73956, .T. ) ;
#128842=ADVANCED_FACE ( 'NONE', ( #102557 ), #135878, .F. ) ;
#128843=DIRECTION ( 'NONE',  ( 1.000000000000000000, 0.000000000000000000, 0.000000000000000000 ) ) ;
#128845=CARTESIAN_POINT ( 'NONE',  ( -10.82816939922345867, 9.759292476615614831, 4.000000000000000000 ) ) ;
#128846=PLANE ( 'NONE',  #25886 ) ;
#128847=LINE ( 'NONE', #18634, #71915 ) ;
#128848=FACE_OUTER_BOUND ( 'NONE', #49169, .T. ) ;
#128849=VECTOR ( 'NONE', #29112, 1000.000000000000000 ) ;
#128852=DIRECTION ( 'NONE',  ( -0.7071067811865486830, 0.7071067811865464625, 0.000000000000000000 ) ) ;
#128854=EDGE_CURVE ( 'NONE', #23121, #95547, #18337, .T. ) ;
#128855=CARTESIAN_POINT ( 'NONE',  ( -6.328169399223490643, 20.25929247661551003, 4.000000000000000000 ) ) ;
#128856=DIRECTION ( 'NONE',  ( -0.6830127018922180770, -0.6830127018922204085, -0.2588190451025213501 ) ) ;
#128857=ORIENTED_EDGE ( 'NONE', *, *, #75588, .T. ) ;
#128859=ORIENTED_EDGE ( 'NONE', *, *, #95489, .F. ) ;
#128860=ORIENTED_EDGE ( 'NONE', *, *, #35527, .T. ) ;
#128861=CARTESIAN_POINT ( 'NONE',  ( -29.56319896779151790, -12.74070752338415247, 9.898150129686444032 ) ) ;
#128862=FACE_OUTER_BOUND ( 'NONE', #42555, .T. ) ;
#128863=VECTOR ( 'NONE', #113839, 1000.000000000000000 ) ;
#128864=LINE ( 'NONE', #85350, #111162 ) ;
#128865=EDGE_CURVE ( 'NONE', #28348, #29516, #114804, .T. ) ;
#128866=CARTESIAN_POINT ( 'NONE',  ( 5.671830600776431197, -6.740707523384218192, 4.000000000000000000 ) ) ;
#128869=VERTEX_POINT ( 'NONE', #136574 ) ;
#128870=VECTOR ( 'NONE', #95133, 1000.000000000000000 ) ;
#128872=CARTESIAN_POINT ( 'NONE',  ( -24.29974487139158867, -27.71228299555223273, 4.000000000000000000 ) ) ;
#128874=AXIS2_PLACEMENT_3D ( 'NONE', #64100, #21311, #130811 ) ;
#128875=LINE ( 'NONE', #75248, #141620 ) ;
#128876=ORIENTED_EDGE ( 'NONE', *, *, #68839, .T. ) ;
#128877=VERTEX_POINT ( 'NONE', #39441 ) ;
#128878=EDGE_LOOP ( 'NONE', ( #128084, #31132, #6005, #122038, #54929, #59509 ) ) ;
#128879=CARTESIAN_POINT ( 'NONE',  ( 2.999999999999975131, 20.58746187583904330, 4.000000000000000000 ) ) ;
#128880=PLANE ( 'NONE',  #2400 ) ;
#128881=LINE ( 'NONE', #95535, #77527 ) ;
#128882=CARTESIAN_POINT ( 'NONE',  ( -11.99999999999991651, 13.55218569542903317, 5.000000000000000000 ) ) ;
#128884=LINE ( 'NONE', #141943, #96624 ) ;
#128885=CARTESIAN_POINT ( 'NONE',  ( 57.18398860626899705, 28.73617430169827358, 5.000000000000000000 ) ) ;
#128888=DIRECTION ( 'NONE',  ( 0.6830127018922181881, 0.6830127018922202975, -0.2588190451025214056 ) ) ;
#128889=LINE ( 'NONE', #39779, #51254 ) ;
#128890=EDGE_LOOP ( 'NONE', ( #37745, #111885, #16351, #29463 ) ) ;
#128891=CARTESIAN_POINT ( 'NONE',  ( 15.18398860626900237, 28.73617430169797871, 5.000000000000000000 ) ) ;
#128892=CARTESIAN_POINT ( 'NONE',  ( -30.79289321881324781, -5.240707523384225297, 5.000000000000000000 ) ) ;
#128893=VERTEX_POINT ( 'NONE', #51741 ) ;
#128894=CARTESIAN_POINT ( 'NONE',  ( 23.01088028653932582, -22.02621442084247860, 4.990779571109218438 ) ) ;
#128895=DIRECTION ( 'NONE',  ( 0.3543493200069162685, -0.000000000000000000, -0.9351131265310288487 ) ) ;
#128896=ORIENTED_EDGE ( 'NONE', *, *, #110621, .F. ) ;
#128898=LINE ( 'NONE', #29581, #12130 ) ;
#128899=LINE ( 'NONE', #29582, #90107 ) ;
#128900=ORIENTED_EDGE ( 'NONE', *, *, #93888, .T. ) ;
#128901=CARTESIAN_POINT ( 'NONE',  ( -54.48921356237310221, -27.52281430457093236, 5.000000000000000000 ) ) ;
#128903=VERTEX_POINT ( 'NONE', #95215 ) ;
#128904=VECTOR ( 'NONE', #107043, 1000.000000000000000 ) ;
#128905=VECTOR ( 'NONE', #105091, 1000.000000000000000 ) ;
#128906=VECTOR ( 'NONE', #53905, 999.9999999999998863 ) ;
#128910=EDGE_CURVE ( 'NONE', #80757, #90561, #16199, .T. ) ;
#128911=PLANE ( 'NONE',  #110971 ) ;
#128912=DIRECTION ( 'NONE',  ( 0.000000000000000000, 1.000000000000000000, 0.000000000000000000 ) ) ;
#128914=EDGE_CURVE ( 'NONE', #88713, #89781, #106796, .T. ) ;
#128915=CARTESIAN_POINT ( 'NONE',  ( 26.99999999999981526, -15.41253812416059432, 4.000000000000000000 ) ) ;
#128916=CARTESIAN_POINT ( 'NONE',  ( -17.81601139373099940, 28.73617430169775133, 5.000000000000000000 ) ) ;
#128917=VECTOR ( 'NONE', #88322, 1000.000000000000000 ) ;
#128918=EDGE_CURVE ( 'NONE', #29177, #6529, #6031, .T. ) ;
#128922=VECTOR ( 'NONE', #24128, 1000.000000000000000 ) ;
#128923=DIRECTION ( 'NONE',  ( 0.7071067811865487940, 0.7071067811865463515, -0.000000000000000000 ) ) ;
#128925=ADVANCED_FACE ( 'NONE', ( #104667 ), #73487, .F. ) ;
#128926=ORIENTED_EDGE ( 'NONE', *, *, #75338, .T. ) ;
#128929=DIRECTION ( 'NONE',  ( 1.000000000000000000, 0.000000000000000000, 0.000000000000000000 ) ) ;
#128932=FACE_OUTER_BOUND ( 'NONE', #101413, .T. ) ;
#128933=CARTESIAN_POINT ( 'NONE',  ( 22.49999999999984013, -2.568876922607788327, 4.000000000000000000 ) ) ;
#128934=FACE_OUTER_BOUND ( 'NONE', #48615, .T. ) ;
#128935=CARTESIAN_POINT ( 'NONE',  ( 0.000000000000000000, 0.000000000000000000, 5.000000000000000000 ) ) ;
#128936=ORIENTED_EDGE ( 'NONE', *, *, #85761, .T. ) ;
#128937=CARTESIAN_POINT ( 'NONE',  ( 3.469446951953614189E-15, 20.96639925780204550, 5.000000000000000000 ) ) ;
#128938=EDGE_CURVE ( 'NONE', #53759, #67529, #29245, .T. ) ;
#128939=DIRECTION ( 'NONE',  ( -0.000000000000000000, 0.3543493200069153248, 0.9351131265310292928 ) ) ;
#128940=LINE ( 'NONE', #129644, #199 ) ;
#128941=EDGE_CURVE ( 'NONE', #82859, #40404, #72817, .T. ) ;
#128942=DIRECTION ( 'NONE',  ( 0.7071067811865486830, -0.7071067811865464625, -0.000000000000000000 ) ) ;
#128943=FACE_OUTER_BOUND ( 'NONE', #104750, .T. ) ;
#128944=ORIENTED_EDGE ( 'NONE', *, *, #27179, .T. ) ;
#128947=DIRECTION ( 'NONE',  ( 0.6830127018922180770, -0.6830127018922204085, -0.2588190451025213501 ) ) ;
#128948=CARTESIAN_POINT ( 'NONE',  ( 11.14818355038138087, 17.25929247661554911, 8.802941693769225751 ) ) ;
#128949=DIRECTION ( 'NONE',  ( -0.000000000000000000, 0.3543493200069153248, 0.9351131265310292928 ) ) ;
#128951=ADVANCED_FACE ( 'NONE', ( #61231 ), #70659, .F. ) ;
#128952=CARTESIAN_POINT ( 'NONE',  ( -10.49999999999992006, 3.052185695429133538, 5.000000000000000000 ) ) ;
#128953=ORIENTED_EDGE ( 'NONE', *, *, #33167, .T. ) ;
#128954=ORIENTED_EDGE ( 'NONE', *, *, #45487, .T. ) ;
#128956=AXIS2_PLACEMENT_3D ( 'NONE', #66410, #55530, #33788 ) ;
#128957=VERTEX_POINT ( 'NONE', #59766 ) ;
#128960=CARTESIAN_POINT ( 'NONE',  ( -3.489213562373097322, -27.52281430457057709, 5.000000000000000000 ) ) ;
#128961=ORIENTED_EDGE ( 'NONE', *, *, #111850, .F. ) ;
#128963=CARTESIAN_POINT ( 'NONE',  ( -12.00548008471251293, 28.92564299267929684, 4.000000000000000000 ) ) ;
#128965=ORIENTED_EDGE ( 'NONE', *, *, #10092, .T. ) ;
#128967=ORIENTED_EDGE ( 'NONE', *, *, #130066, .T. ) ;
#128968=CARTESIAN_POINT ( 'NONE',  ( 33.70710678118631165, 5.259292476615667233, 5.000000000000000000 ) ) ;
#128969=EDGE_CURVE ( 'NONE', #47934, #81908, #49621, .T. ) ;
#128970=AXIS2_PLACEMENT_3D ( 'NONE', #66884, #3036, #88649 ) ;
#128974=ORIENTED_EDGE ( 'NONE', *, *, #23398, .F. ) ;
#128975=ORIENTED_EDGE ( 'NONE', *, *, #58814, .F. ) ;
#128976=DIRECTION ( 'NONE',  ( 0.7071067811865487940, 0.7071067811865463515, 0.000000000000000000 ) ) ;
#128981=VECTOR ( 'NONE', #71254, 1000.000000000000000 ) ;
#128982=ORIENTED_EDGE ( 'NONE', *, *, #107825, .F. ) ;
#128983=CARTESIAN_POINT ( 'NONE',  ( -13.24976746729824129, 4.588264127556670680, 4.661243073242808066 ) ) ;
#128984=EDGE_CURVE ( 'NONE', #67467, #137150, #116266, .T. ) ;
#128985=ORIENTED_EDGE ( 'NONE', *, *, #58959, .T. ) ;
#128987=CARTESIAN_POINT ( 'NONE',  ( -8.999999999999952038, -16.02097659208073566, -11.96015758381207128 ) ) ;
#128988=DIRECTION ( 'NONE',  ( 0.7071067811865487940, 0.7071067811865463515, 0.000000000000000000 ) ) ;
#128989=VERTEX_POINT ( 'NONE', #84381 ) ;
#128990=DIRECTION ( 'NONE',  ( -0.7071067811865486830, -0.7071067811865464625, -0.000000000000000000 ) ) ;
#128991=EDGE_CURVE ( 'NONE', #127597, #138729, #128569, .T. ) ;
#128992=CARTESIAN_POINT ( 'NONE',  ( 13.49999999999991473, 5.696342897626525570, -7.587980461218370998 ) ) ;
#128993=PLANE ( 'NONE',  #78516 ) ;
#128994=CARTESIAN_POINT ( 'NONE',  ( 11.51078643762690490, -27.52281430457047406, 5.000000000000000000 ) ) ;
#128995=ORIENTED_EDGE ( 'NONE', *, *, #129595, .F. ) ;
#128996=LINE ( 'NONE', #73914, #115801 ) ;
#128997=VECTOR ( 'NONE', #110067, 999.9999999999998863 ) ;
#128998=FACE_BOUND ( 'NONE', #7847, .T. ) ;
#128999=EDGE_LOOP ( 'NONE', ( #47203, #83872, #115015, #91428 ) ) ;
#129000=LINE ( 'NONE', #128315, #29519 ) ;
#129001=CARTESIAN_POINT ( 'NONE',  ( -27.32816939922333432, -12.74070752338415247, 4.000000000000000000 ) ) ;
#129003=LINE ( 'NONE', #96342, #107039 ) ;
#129004=ORIENTED_EDGE ( 'NONE', *, *, #124533, .F. ) ;
#129005=CARTESIAN_POINT ( 'NONE',  ( -51.18398860626899705, 28.73617430169823095, 5.000000000000000000 ) ) ;
#129006=VERTEX_POINT ( 'NONE', #82934 ) ;
#129007=ORIENTED_EDGE ( 'NONE', *, *, #43413, .F. ) ;
#129008=VECTOR ( 'NONE', #133805, 1000.000000000000000 ) ;
#129009=ORIENTED_EDGE ( 'NONE', *, *, #139487, .T. ) ;
#129011=VECTOR ( 'NONE', #32703, 1000.000000000000227 ) ;
#129012=PLANE ( 'NONE',  #39649 ) ;
#129013=CARTESIAN_POINT ( 'NONE',  ( 11.81601139373100651, 28.73617430169779041, 5.000000000000000000 ) ) ;
#129014=CARTESIAN_POINT ( 'NONE',  ( 18.48921356237309510, -27.52281430457068367, 5.000000000000000000 ) ) ;
#129015=CARTESIAN_POINT ( 'NONE',  ( 8.700255128608413102, -27.71228299555199825, 4.000000000000000000 ) ) ;
#129016=CARTESIAN_POINT ( 'NONE',  ( 30.48921356237309510, -27.52281430457076894, 5.000000000000000000 ) ) ;
#129017=CARTESIAN_POINT ( 'NONE',  ( 1.499999999999980460, 1.030536316426505117, -5.498701923753805509 ) ) ;
#129018=VECTOR ( 'NONE', #33954, 1000.000000000000000 ) ;
#129019=CARTESIAN_POINT ( 'NONE',  ( 48.18398860626899705, 28.73617430169820608, 5.000000000000000000 ) ) ;
#129021=ADVANCED_FACE ( 'NONE', ( #82239 ), #126413, .T. ) ;
#129022=DIRECTION ( 'NONE',  ( 0.7071067811865487940, 0.7071067811865463515, 0.000000000000000000 ) ) ;
#129023=PLANE ( 'NONE',  #33194 ) ;
#129024=ORIENTED_EDGE ( 'NONE', *, *, #7060, .T. ) ;
#129026=VERTEX_POINT ( 'NONE', #66185 ) ;
#129027=ORIENTED_EDGE ( 'NONE', *, *, #60791, .F. ) ;
#129028=CARTESIAN_POINT ( 'NONE',  ( -19.05000000000000071, 3.174999999999997158, 5.000000000000000000 ) ) ;
#129030=EDGE_LOOP ( 'NONE', ( #141913, #32012, #71619, #128965 ) ) ;
#129032=DIRECTION ( 'NONE',  ( 1.000000000000000000, 0.000000000000000000, 0.000000000000000000 ) ) ;
#129033=CARTESIAN_POINT ( 'NONE',  ( 34.42499999999998295, -1.458600742197942779, 5.000000000000000000 ) ) ;
#129035=EDGE_CURVE ( 'NONE', #58614, #52888, #52421, .T. ) ;
#129036=CARTESIAN_POINT ( 'NONE',  ( 0.3281693992235185098, 20.25929247661552068, 4.000000000000000000 ) ) ;
#129037=ORIENTED_EDGE ( 'NONE', *, *, #45160, .T. ) ;
#129039=DIRECTION ( 'NONE',  ( -0.7071067811865486830, -0.7071067811865464625, -0.000000000000000000 ) ) ;
#129040=ORIENTED_EDGE ( 'NONE', *, *, #105482, .T. ) ;
#129042=CARTESIAN_POINT ( 'NONE',  ( 34.42499999999998295, -21.72500000000000142, 4.500000000000000888 ) ) ;
#129045=ORIENTED_EDGE ( 'NONE', *, *, #125279, .F. ) ;
#129047=DIRECTION ( 'NONE',  ( -0.7071067811865486830, -0.7071067811865464625, 0.000000000000000000 ) ) ;
#129048=VERTEX_POINT ( 'NONE', #131434 ) ;
#129049=ORIENTED_EDGE ( 'NONE', *, *, #129621, .F. ) ;
#129050=DIRECTION ( 'NONE',  ( -0.7071067811865487940, 0.7071067811865463515, -0.000000000000000000 ) ) ;
#129051=VERTEX_POINT ( 'NONE', #121249 ) ;
#129052=VECTOR ( 'NONE', #35936, 1000.000000000000000 ) ;
#129053=FACE_OUTER_BOUND ( 'NONE', #139110, .T. ) ;
#129054=LINE ( 'NONE', #75411, #13977 ) ;
#129055=DIRECTION ( 'NONE',  ( 0.7071067811865487940, 0.7071067811865463515, -0.000000000000000000 ) ) ;
#129056=CARTESIAN_POINT ( 'NONE',  ( -14.99999999999989875, -6.108550654416973202, -3.114665004255002589 ) ) ;
#129057=EDGE_CURVE ( 'NONE', #84757, #41451, #42300, .T. ) ;
#129059=DIRECTION ( 'NONE',  ( -0.7071067811865487940, 0.7071067811865463515, -0.000000000000000000 ) ) ;
#129060=( BOUNDED_CURVE ( )  B_SPLINE_CURVE ( 3, ( #62508, #42899, #18980, #131314 ),
 .UNSPECIFIED., .F., .T. ) 
 B_SPLINE_CURVE_WITH_KNOTS ( ( 4, 4 ),
 ( 1.208578181583235267, 1.359146454359429379 ),
 .UNSPECIFIED. ) 
 CURVE ( )  GEOMETRIC_REPRESENTATION_ITEM ( )  RATIONAL_B_SPLINE_CURVE ( ( 1.000000000000000000, 0.9981116584018954185, 0.9981116584018954185, 1.000000000000000000 ) ) 
 REPRESENTATION_ITEM ( '' )  );
#129061=CARTESIAN_POINT ( 'NONE',  ( 0.000000000000000000, 0.000000000000000000, 5.000000000000000000 ) ) ;
#129062=CARTESIAN_POINT ( 'NONE',  ( -27.18398860626900060, 28.73617430169806042, 5.000000000000000000 ) ) ;
#129063=VECTOR ( 'NONE', #85408, 1000.000000000000000 ) ;
#129064=ORIENTED_EDGE ( 'NONE', *, *, #136760, .T. ) ;
#129065=LINE ( 'NONE', #86303, #88307 ) ;
#129066=CARTESIAN_POINT ( 'NONE',  ( -0.2997448713915885632, -27.71228299555206220, 4.000000000000000000 ) ) ;
#129067=EDGE_LOOP ( 'NONE', ( #49781, #5963, #76856 ) ) ;
#129069=DIRECTION ( 'NONE',  ( 0.6830127018922181881, 0.6830127018922202975, -0.2588190451025214056 ) ) ;
#129070=ORIENTED_EDGE ( 'NONE', *, *, #115451, .F. ) ;
#129071=VERTEX_POINT ( 'NONE', #21939 ) ;
#129072=CARTESIAN_POINT ( 'NONE',  ( 0.000000000000000000, 0.000000000000000000, 5.000000000000000000 ) ) ;
#129073=LINE ( 'NONE', #84865, #55366 ) ;
#129074=ORIENTED_EDGE ( 'NONE', *, *, #44322, .T. ) ;
#129075=CARTESIAN_POINT ( 'NONE',  ( 0.6684674115985667076, -18.74070752338408496, 20.73178291233841009 ) ) ;
#129077=CARTESIAN_POINT ( 'NONE',  ( 14.21837311707495743, 21.74787736706806740, 4.999607392498049308 ) ) ;
#129078=ADVANCED_FACE ( 'NONE', ( #141596 ), #43004, .F. ) ;
#129079=AXIS2_PLACEMENT_3D ( 'NONE', #48599, #81248, #60205 ) ;
#129080=DIRECTION ( 'NONE',  ( -0.000000000000000000, 0.000000000000000000, 1.000000000000000000 ) ) ;
#129081=ADVANCED_FACE ( 'NONE', ( #95933 ), #140170, .F. ) ;
#129083=LINE ( 'NONE', #19612, #65229 ) ;
#129084=PLANE ( 'NONE',  #30924 ) ;
#129085=FACE_OUTER_BOUND ( 'NONE', #40432, .T. ) ;
#129086=DIRECTION ( 'NONE',  ( 0.6830127018922180770, -0.6830127018922204085, -0.2588190451025213501 ) ) ;
#129087=CARTESIAN_POINT ( 'NONE',  ( -29.20710678118632586, -11.24070752338416668, 5.000000000000000000 ) ) ;
#129088=DIRECTION ( 'NONE',  ( -0.7071067811865487940, 0.7071067811865463515, 0.000000000000000000 ) ) ;
#129089=DIRECTION ( 'NONE',  ( -0.7071067811865486830, -0.7071067811865464625, -0.000000000000000000 ) ) ;
#129091=EDGE_CURVE ( 'NONE', #51626, #96824, #67456, .T. ) ;
#129093=EDGE_CURVE ( 'NONE', #80606, #126512, #30708, .T. ) ;
#129094=ORIENTED_EDGE ( 'NONE', *, *, #69355, .T. ) ;
#129098=ORIENTED_EDGE ( 'NONE', *, *, #91169, .F. ) ;
#129099=ORIENTED_EDGE ( 'NONE', *, *, #87375, .F. ) ;
#129100=DIRECTION ( 'NONE',  ( -0.7071067811865486830, 0.7071067811865464625, 0.000000000000000000 ) ) ;
#129101=CARTESIAN_POINT ( 'NONE',  ( 34.91107144025653497, 21.84219451764873909, 4.000000000000000000 ) ) ;
#129102=ORIENTED_EDGE ( 'NONE', *, *, #50229, .F. ) ;
#129103=VECTOR ( 'NONE', #34022, 1000.000000000000000 ) ;
#129104=CARTESIAN_POINT ( 'NONE',  ( -6.005480084712508493, 28.92564299267933947, 4.000000000000000000 ) ) ;
#129105=CARTESIAN_POINT ( 'NONE',  ( -25.99806943317883423, -22.22500000000000142, 4.500000000000000888 ) ) ;
#129106=EDGE_CURVE ( 'NONE', #30609, #93894, #140849, .T. ) ;
#129107=LINE ( 'NONE', #29786, #32576 ) ;
#129108=DIRECTION ( 'NONE',  ( -0.3543493200069162685, -0.000000000000000000, -0.9351131265310288487 ) ) ;
#129110=ORIENTED_EDGE ( 'NONE', *, *, #42728, .T. ) ;
#129111=EDGE_CURVE ( 'NONE', #68534, #105207, #32112, .T. ) ;
#129112=APPLICATION_CONTEXT ( 'automotive_design' ) ;
#129113=LINE ( 'NONE', #27652, #76596 ) ;
#129115=CARTESIAN_POINT ( 'NONE',  ( 63.48921356237309510, -27.52281430457099631, 5.000000000000000000 ) ) ;
#129116=VECTOR ( 'NONE', #26836, 1000.000000000000000 ) ;
#129118=PLANE ( 'NONE',  #53863 ) ;
#129119=CARTESIAN_POINT ( 'NONE',  ( 7.499999999999949374, 21.05218569542895324, 5.000000000000000000 ) ) ;
#129120=VECTOR ( 'NONE', #69115, 1000.000000000000000 ) ;
#129121=DIRECTION ( 'NONE',  ( -0.000000000000000000, 0.000000000000000000, 1.000000000000000000 ) ) ;
#129122=EDGE_CURVE ( 'NONE', #91522, #54031, #31405, .T. ) ;
#129123=DIRECTION ( 'NONE',  ( -0.000000000000000000, 0.000000000000000000, 1.000000000000000000 ) ) ;
#129124=LINE ( 'NONE', #131811, #136470 ) ;
#129125=VERTEX_POINT ( 'NONE', #118388 ) ;
#129126=ORIENTED_EDGE ( 'NONE', *, *, #23351, .T. ) ;
#129128=VERTEX_POINT ( 'NONE', #63352 ) ;
#129130=CARTESIAN_POINT ( 'NONE',  ( 0.005480084712502889671, 28.92564299267938210, 4.000000000000000000 ) ) ;
#129132=EDGE_CURVE ( 'NONE', #117635, #108859, #74932, .T. ) ;
#129133=DIRECTION ( 'NONE',  ( 0.7071067811865487940, 0.7071067811865463515, 0.000000000000000000 ) ) ;
#129134=DIRECTION ( 'NONE',  ( 0.6830127018922180770, -0.6830127018922204085, -0.2588190451025213501 ) ) ;
#129138=ORIENTED_EDGE ( 'NONE', *, *, #119802, .F. ) ;
#129139=CARTESIAN_POINT ( 'NONE',  ( -15.18398860626900237, 28.73617430169797871, 5.000000000000000000 ) ) ;
#129140=ORIENTED_EDGE ( 'NONE', *, *, #39987, .F. ) ;
#129141=EDGE_CURVE ( 'NONE', #71727, #116539, #8181, .T. ) ;
#129142=DIRECTION ( 'NONE',  ( -0.7071067811865486830, 0.7071067811865464625, 0.000000000000000000 ) ) ;
#129143=DIRECTION ( 'NONE',  ( -0.6830127018922181881, 0.6830127018922202975, -0.2588190451025214056 ) ) ;
#129144=CARTESIAN_POINT ( 'NONE',  ( 60.29974487139158867, -27.71228299555248142, 4.000000000000000000 ) ) ;
#129145=CARTESIAN_POINT ( 'NONE',  ( 29.22995720542186149, 21.73644205237998506, 5.000000000000000888 ) ) ;
#129146=EDGE_LOOP ( 'NONE', ( #56353, #87381, #83633, #108331 ) ) ;
#129148=ORIENTED_EDGE ( 'NONE', *, *, #13634, .T. ) ;
#129149=DIRECTION ( 'NONE',  ( -0.000000000000000000, 0.000000000000000000, 1.000000000000000000 ) ) ;
#129150=CARTESIAN_POINT ( 'NONE',  ( 20.99999999999985789, 11.96639925780214320, 5.000000000000000000 ) ) ;
#129151=CARTESIAN_POINT ( 'NONE',  ( -81.48921356237309510, -27.52281430457112066, 5.000000000000000000 ) ) ;
#129152=EDGE_CURVE ( 'NONE', #101337, #80109, #98088, .T. ) ;
#129153=AXIS2_PLACEMENT_3D ( 'NONE', #85497, #18079, #105816 ) ;
#129154=CARTESIAN_POINT ( 'NONE',  ( 36.29974487139159578, -27.71228299555231445, 4.000000000000000000 ) ) ;
#129155=EDGE_CURVE ( 'NONE', #55245, #43089, #142322, .T. ) ;
#129157=VERTEX_POINT ( 'NONE', #119800 ) ;
#129158=CARTESIAN_POINT ( 'NONE',  ( -36.48921356237310221, -27.52281430457080802, 5.000000000000000000 ) ) ;
#129160=ORIENTED_EDGE ( 'NONE', *, *, #126146, .F. ) ;
#129161=ORIENTED_EDGE ( 'NONE', *, *, #107641, .F. ) ;
#129162=( BOUNDED_CURVE ( )  B_SPLINE_CURVE ( 3, ( #137590, #136147, #39721, #7012 ),
 .UNSPECIFIED., .F., .F. ) 
 B_SPLINE_CURVE_WITH_KNOTS ( ( 4, 4 ),
 ( 5.143245962375964986, 6.645403452391246191 ),
 .UNSPECIFIED. ) 
 CURVE ( )  GEOMETRIC_REPRESENTATION_ITEM ( )  RATIONAL_B_SPLINE_CURVE ( ( 1.000000000000000000, 0.8206354192515240564, 0.8206354192515240564, 1.000000000000000000 ) ) 
 REPRESENTATION_ITEM ( '' )  );
#129163=VERTEX_POINT ( 'NONE', #32852 ) ;
#129164=CARTESIAN_POINT ( 'NONE',  ( 11.99451991528749417, 28.92564299267946382, 4.000000000000000000 ) ) ;
#129165=LINE ( 'NONE', #29847, #139186 ) ;
#129166=FACE_BOUND ( 'NONE', #62819, .T. ) ;
#129170=ORIENTED_EDGE ( 'NONE', *, *, #40155, .T. ) ;
#129171=LINE ( 'NONE', #75528, #50382 ) ;
#129172=VERTEX_POINT ( 'NONE', #20492 ) ;
#129173=ORIENTED_EDGE ( 'NONE', *, *, #4451, .T. ) ;
#129174=CARTESIAN_POINT ( 'NONE',  ( -4.171830600776436526, 9.759292476615614831, 4.000000000000000000 ) ) ;
#129175=ORIENTED_EDGE ( 'NONE', *, *, #134532, .F. ) ;
#129178=VECTOR ( 'NONE', #72006, 1000.000000000000227 ) ;
#129179=LINE ( 'NONE', #29864, #16294 ) ;
#129180=PLANE ( 'NONE',  #125987 ) ;
#129182=ORIENTED_EDGE ( 'NONE', *, *, #11334, .F. ) ;
#129183=ADVANCED_FACE ( 'NONE', ( #65490 ), #98774, .F. ) ;
#129184=LINE ( 'NONE', #19011, #101142 ) ;
#129185=CARTESIAN_POINT ( 'NONE',  ( -7.171830600776425868, 12.75929247661559529, 4.000000000000000000 ) ) ;
#129186=DIRECTION ( 'NONE',  ( 0.7071067811865487940, 0.7071067811865463515, 0.000000000000000000 ) ) ;
#129188=DIRECTION ( 'NONE',  ( 0.7071067811865487940, 0.7071067811865463515, 0.000000000000000000 ) ) ;
#129189=ORIENTED_EDGE ( 'NONE', *, *, #3135, .F. ) ;
#129192=VECTOR ( 'NONE', #72226, 999.9999999999998863 ) ;
#129193=DIRECTION ( 'NONE',  ( -0.7071067811865486830, 0.7071067811865464625, 0.000000000000000000 ) ) ;
#129195=ORIENTED_EDGE ( 'NONE', *, *, #106297, .F. ) ;
#129196=VECTOR ( 'NONE', #7556, 1000.000000000000114 ) ;
#129197=VERTEX_POINT ( 'NONE', #24794 ) ;
#129198=CARTESIAN_POINT ( 'NONE',  ( 5.292986735706907808, -21.74070752338406365, 4.999753212805221558 ) ) ;
#129200=EDGE_CURVE ( 'NONE', #135168, #11025, #55306, .T. ) ;
#129201=EDGE_CURVE ( 'NONE', #85105, #64105, #102392, .T. ) ;
#129202=DIRECTION ( 'NONE',  ( -0.000000000000000000, -0.000000000000000000, 1.000000000000000000 ) ) ;
#129203=ORIENTED_EDGE ( 'NONE', *, *, #112869, .F. ) ;
#129204=CARTESIAN_POINT ( 'NONE',  ( -4.499999999999959144, -14.94781430457067373, 5.000000000000000000 ) ) ;
#129209=DIRECTION ( 'NONE',  ( 0.7071067811865486830, -0.7071067811865464625, -0.000000000000000000 ) ) ;
#129210=ORIENTED_EDGE ( 'NONE', *, *, #92887, .F. ) ;
#129213=DIRECTION ( 'NONE',  ( -0.7071067811865486830, 0.7071067811865463515, 0.000000000000000000 ) ) ;
#129214=FACE_OUTER_BOUND ( 'NONE', #11886, .T. ) ;
#129215=DIRECTION ( 'NONE',  ( -0.6830127018922180770, -0.6830127018922204085, -0.2588190451025213501 ) ) ;
#129216=VERTEX_POINT ( 'NONE', #99480 ) ;
#129217=CARTESIAN_POINT ( 'NONE',  ( -15.18398860626900237, 28.73617430169797871, 5.000000000000000000 ) ) ;
#129218=ORIENTED_EDGE ( 'NONE', *, *, #135486, .T. ) ;
#129219=LINE ( 'NONE', #19755, #24115 ) ;
#129220=CARTESIAN_POINT ( 'NONE',  ( 0.000000000000000000, -21.72500000000000142, 4.500000000000000888 ) ) ;
#129221=LINE ( 'NONE', #118344, #35613 ) ;
#129222=ADVANCED_FACE ( 'NONE', ( #22621 ), #11758, .F. ) ;
#129223=ORIENTED_EDGE ( 'NONE', *, *, #75860, .F. ) ;
#129224=DIRECTION ( 'NONE',  ( -0.7071067811865486830, 0.7071067811865464625, 0.000000000000000000 ) ) ;
#129225=PLANE ( 'NONE',  #120580 ) ;
#129226=CARTESIAN_POINT ( 'NONE',  ( 24.66846741159842082, -18.74070752338409562, 20.73178291233847048 ) ) ;
#129228=VECTOR ( 'NONE', #116623, 1000.000000000000227 ) ;
#129229=EDGE_CURVE ( 'NONE', #5611, #95146, #100232, .T. ) ;
#129230=DIRECTION ( 'NONE',  ( -0.6830127018922181881, 0.6830127018922202975, -0.2588190451025214056 ) ) ;
#129231=CARTESIAN_POINT ( 'NONE',  ( 21.18398860626899349, 28.73617430169802134, 5.000000000000000000 ) ) ;
#129232=DIRECTION ( 'NONE',  ( -0.3543493200069162685, -0.000000000000000000, -0.9351131265310288487 ) ) ;
#129233=VECTOR ( 'NONE', #10317, 1000.000000000000000 ) ;
#129234=CARTESIAN_POINT ( 'NONE',  ( -33.48921356237309510, -27.52281430457078670, 5.000000000000000000 ) ) ;
#129235=LINE ( 'NONE', #29921, #11351 ) ;
#129236=ORIENTED_EDGE ( 'NONE', *, *, #94771, .T. ) ;
#129237=ORIENTED_EDGE ( 'NONE', *, *, #49867, .T. ) ;
#129239=CARTESIAN_POINT ( 'NONE',  ( 11.99999999999992006, 5.966399257802200040, 5.000000000000000000 ) ) ;
#129241=DIRECTION ( 'NONE',  ( -0.000000000000000000, 0.3543493200069153248, 0.9351131265310291818 ) ) ;
#129242=DIRECTION ( 'NONE',  ( -0.3543493200069163240, -0.000000000000000000, -0.9351131265310288487 ) ) ;
#129246=DIRECTION ( 'NONE',  ( 0.6830127018922181881, 0.6830127018922202975, -0.2588190451025214056 ) ) ;
#129248=LINE ( 'NONE', #30687, #21495 ) ;
#129250=FACE_OUTER_BOUND ( 'NONE', #121078, .T. ) ;
#129252=DIRECTION ( 'NONE',  ( -0.7071067811865487940, 0.7071067811865463515, -0.000000000000000000 ) ) ;
#129253=VECTOR ( 'NONE', #19951, 1000.000000000000000 ) ;
#129254=ADVANCED_FACE ( 'NONE', ( #151 ), #91504, .T. ) ;
#129255=EDGE_CURVE ( 'NONE', #56732, #126282, #123442, .T. ) ;
#129256=VERTEX_POINT ( 'NONE', #66888 ) ;
#129257=LINE ( 'NONE', #116964, #102046 ) ;
#129258=EDGE_LOOP ( 'NONE', ( #142162, #56748, #91679, #58643 ) ) ;
#129259=ORIENTED_EDGE ( 'NONE', *, *, #118218, .F. ) ;
#129261=DIRECTION ( 'NONE',  ( -0.7071067811865486830, -0.7071067811865464625, -0.000000000000000000 ) ) ;
#129262=ADVANCED_FACE ( 'NONE', ( #13184 ), #57458, .T. ) ;
#129263=DIRECTION ( 'NONE',  ( -0.000000000000000000, 0.000000000000000000, 1.000000000000000000 ) ) ;
#129264=DIRECTION ( 'NONE',  ( 0.6830127018922181881, 0.6830127018922202975, -0.2588190451025214056 ) ) ;
#129265=LINE ( 'NONE', #53130, #129663 ) ;
#129267=DIRECTION ( 'NONE',  ( -0.3543493200069162685, -0.000000000000000000, -0.9351131265310288487 ) ) ;
#129268=DIRECTION ( 'NONE',  ( 0.7071067811865486830, -0.7071067811865464625, -0.000000000000000000 ) ) ;
#129269=VERTEX_POINT ( 'NONE', #880 ) ;
#129270=ADVANCED_FACE ( 'NONE', ( #111066 ), #67633, .F. ) ;
#129271=DIRECTION ( 'NONE',  ( 0.6830127018922180770, -0.6830127018922204085, -0.2588190451025213501 ) ) ;
#129272=LINE ( 'NONE', #140855, #72336 ) ;
#129273=DIRECTION ( 'NONE',  ( -1.000000000000000000, 0.000000000000000000, 0.000000000000000000 ) ) ;
#129274=CARTESIAN_POINT ( 'NONE',  ( -6.489213562373093325, -27.52281430457059841, 5.000000000000000000 ) ) ;
#129275=CARTESIAN_POINT ( 'NONE',  ( -5.207106781186501721, -14.24070752338413293, 5.000000000000000000 ) ) ;
#129276=CARTESIAN_POINT ( 'NONE',  ( -26.99999999999980460, 14.58746187583909837, 4.000000000000000000 ) ) ;
#129279=DIRECTION ( 'NONE',  ( 0.7071067811865486830, -0.7071067811865464625, -0.000000000000000000 ) ) ;
#129281=ORIENTED_EDGE ( 'NONE', *, *, #30960, .F. ) ;
#129283=ADVANCED_FACE ( 'NONE', ( #62996 ), #39072, .T. ) ;
#129284=DIRECTION ( 'NONE',  ( -0.3543493200069163240, 0.000000000000000000, 0.9351131265310288487 ) ) ;
#129285=CARTESIAN_POINT ( 'NONE',  ( 29.99999999999979039, -21.84840872380821963, 2.849755605029675731 ) ) ;
#129286=CARTESIAN_POINT ( 'NONE',  ( 19.49999999999986500, -15.29013452822852770, 0.3645803511610800074 ) ) ;
#129287=VERTEX_POINT ( 'NONE', #19457 ) ;
#129288=EDGE_CURVE ( 'NONE', #56372, #23069, #8529, .T. ) ;
#129289=CARTESIAN_POINT ( 'NONE',  ( -8.816011393731004731, 28.73617430169781173, 5.000000000000000000 ) ) ;
#129291=VERTEX_POINT ( 'NONE', #106423 ) ;
#129294=ORIENTED_EDGE ( 'NONE', *, *, #42513, .T. ) ;
#129295=DIRECTION ( 'NONE',  ( -0.6830127018922181881, 0.6830127018922202975, -0.2588190451025214056 ) ) ;
#129296=VECTOR ( 'NONE', #141292, 999.9999999999998863 ) ;
#129297=VECTOR ( 'NONE', #62218, 1000.000000000000000 ) ;
#129298=AXIS2_PLACEMENT_3D ( 'NONE', #53778, #121835, #66778 ) ;
#129300=FACE_OUTER_BOUND ( 'NONE', #23192, .T. ) ;
#129301=VECTOR ( 'NONE', #141484, 1000.000000000000227 ) ;
#129302=CARTESIAN_POINT ( 'NONE',  ( -28.49999999999979750, 7.466399257802189382, 5.000000000000000000 ) ) ;
#129303=ORIENTED_EDGE ( 'NONE', *, *, #79310, .F. ) ;
#129304=CARTESIAN_POINT ( 'NONE',  ( -9.328169399223463998, -12.74070752338415780, 4.000000000000000000 ) ) ;
#129306=DIRECTION ( 'NONE',  ( -0.3543493200069162685, -0.000000000000000000, -0.9351131265310288487 ) ) ;
#129307=EDGE_LOOP ( 'NONE', ( #34894, #37474, #106745, #108952 ) ) ;
#129308=CARTESIAN_POINT ( 'NONE',  ( -28.59167451900981405, -0.7407075233842735917, 14.76736230305374065 ) ) ;
#129309=CARTESIAN_POINT ( 'NONE',  ( 23.99451991528749062, 28.92564299267954908, 4.000000000000000000 ) ) ;
#129310=EDGE_CURVE ( 'NONE', #116472, #21645, #74574, .T. ) ;
#129312=CARTESIAN_POINT ( 'NONE',  ( 24.29177708983032957, -15.74070752338412049, 19.73771281079103446 ) ) ;
#129314=EDGE_CURVE ( 'NONE', #122713, #43483, #63703, .T. ) ;
#129315=EDGE_LOOP ( 'NONE', ( #93920, #141132, #21984, #29904 ) ) ;
#129316=ADVANCED_FACE ( 'NONE', ( #31072 ), #94150, .T. ) ;
#129317=ORIENTED_EDGE ( 'NONE', *, *, #117813, .T. ) ;
#129319=DIRECTION ( 'NONE',  ( 1.000000000000000000, 0.000000000000000000, 0.000000000000000000 ) ) ;
#129320=LINE ( 'NONE', #107572, #121853 ) ;
#129321=LINE ( 'NONE', #74251, #105697 ) ;
#129322=VERTEX_POINT ( 'NONE', #127507 ) ;
#129323=ORIENTED_EDGE ( 'NONE', *, *, #87263, .T. ) ;
#129325=PLANE ( 'NONE',  #60792 ) ;
#129326=CARTESIAN_POINT ( 'NONE',  ( -21.18398860626899349, 28.73617430169802134, 5.000000000000000000 ) ) ;
#129329=ORIENTED_EDGE ( 'NONE', *, *, #110667, .T. ) ;
#129330=VECTOR ( 'NONE', #136591, 1000.000000000000000 ) ;
#129331=CARTESIAN_POINT ( 'NONE',  ( -6.643187427517349697, -20.24070752338407786, 21.22881796311211389 ) ) ;
#129332=ORIENTED_EDGE ( 'NONE', *, *, #63006, .F. ) ;
#129333=DIRECTION ( 'NONE',  ( -0.000000000000000000, 0.000000000000000000, 1.000000000000000000 ) ) ;
#129334=CARTESIAN_POINT ( 'NONE',  ( -34.92500000000001137, -22.22500000000000142, 4.500000000000000888 ) ) ;
#129335=VECTOR ( 'NONE', #76154, 1000.000000000000000 ) ;
#129337=AXIS2_PLACEMENT_3D ( 'NONE', #20844, #89680, #65840 ) ;
#129338=AXIS2_PLACEMENT_3D ( 'NONE', #103002, #105820, #115988 ) ;
#129339=DIRECTION ( 'NONE',  ( 0.7071067811865487940, 0.7071067811865463515, 0.000000000000000000 ) ) ;
#129340=FACE_BOUND ( 'NONE', #51891, .T. ) ;
#129341=CARTESIAN_POINT ( 'NONE',  ( -11.20710678118645731, -14.24070752338412937, 5.000000000000000000 ) ) ;
#129343=DIRECTION ( 'NONE',  ( -0.7071067811865487940, 0.7071067811865463515, -0.000000000000000000 ) ) ;
#129345=ORIENTED_EDGE ( 'NONE', *, *, #136320, .T. ) ;
#129347=VECTOR ( 'NONE', #135316, 1000.000000000000000 ) ;
#129349=ORIENTED_EDGE ( 'NONE', *, *, #91430, .T. ) ;
#129351=ORIENTED_EDGE ( 'NONE', *, *, #65697, .F. ) ;
#129352=CARTESIAN_POINT ( 'NONE',  ( -38.99451991528749062, 28.92564299267965211, 4.000000000000000000 ) ) ;
#129353=PLANE ( 'NONE',  #25730 ) ;
#129354=EDGE_CURVE ( 'NONE', #80143, #120101, #17312, .T. ) ;
#129356=CARTESIAN_POINT ( 'NONE',  ( 20.99999999999985079, -16.60178936734446609, 0.8616154019347975757 ) ) ;
#129357=VECTOR ( 'NONE', #6169, 1000.000000000000000 ) ;
#129358=FACE_OUTER_BOUND ( 'NONE', #6195, .T. ) ;
#129359=LINE ( 'NONE', #41641, #53022 ) ;
#129360=LINE ( 'NONE', #143105, #13064 ) ;
#129361=CARTESIAN_POINT ( 'NONE',  ( -18.18398860626898994, 28.73617430169800002, 5.000000000000000000 ) ) ;
#129363=DIRECTION ( 'NONE',  ( -0.6830127018922180770, -0.6830127018922204085, -0.2588190451025213501 ) ) ;
#129364=DIRECTION ( 'NONE',  ( -0.7071067811865486830, 0.7071067811865464625, 0.000000000000000000 ) ) ;
#129365=DIRECTION ( 'NONE',  ( -0.000000000000000000, 0.000000000000000000, 1.000000000000000000 ) ) ;
#129369=ORIENTED_EDGE ( 'NONE', *, *, #116883, .T. ) ;
#129370=ORIENTED_EDGE ( 'NONE', *, *, #138594, .F. ) ;
#129371=EDGE_CURVE ( 'NONE', #52857, #33478, #84718, .T. ) ;
#129372=ORIENTED_EDGE ( 'NONE', *, *, #84434, .T. ) ;
#129374=ORIENTED_EDGE ( 'NONE', *, *, #36606, .T. ) ;
#129376=ADVANCED_FACE ( 'NONE', ( #17989 ), #139845, .T. ) ;
#129377=EDGE_CURVE ( 'NONE', #68934, #48693, #1285, .T. ) ;
#129381=EDGE_CURVE ( 'NONE', #84436, #79777, #64391, .T. ) ;
#129382=FACE_OUTER_BOUND ( 'NONE', #89075, .T. ) ;
#129383=ORIENTED_EDGE ( 'NONE', *, *, #21387, .T. ) ;
#129384=CARTESIAN_POINT ( 'NONE',  ( -21.64318742751725821, -20.24070752338407075, 21.22881796311207836 ) ) ;
#129385=FACE_OUTER_BOUND ( 'NONE', #25240, .T. ) ;
#129386=DIRECTION ( 'NONE',  ( -0.7071067811865487940, 0.7071067811865463515, 0.000000000000000000 ) ) ;
#129387=ORIENTED_EDGE ( 'NONE', *, *, #24513, .T. ) ;
#129388=ORIENTED_EDGE ( 'NONE', *, *, #134725, .F. ) ;
#129389=LINE ( 'NONE', #76477, #93173 ) ;
#129390=CARTESIAN_POINT ( 'NONE',  ( -25.11017322888192993, -22.22500000000000142, 4.785647885939352086 ) ) ;
#129391=ADVANCED_FACE ( 'NONE', ( #86870 ), #31768, .T. ) ;
#129392=ORIENTED_EDGE ( 'NONE', *, *, #85085, .F. ) ;
#129393=PLANE ( 'NONE',  #101366 ) ;
#129397=EDGE_LOOP ( 'NONE', ( #127530, #49626, #11388, #49214 ) ) ;
#129398=DIRECTION ( 'NONE',  ( 1.000000000000000000, 0.000000000000000000, 0.000000000000000000 ) ) ;
#129399=AXIS2_PLACEMENT_3D ( 'NONE', #66070, #10220, #55906 ) ;
#129400=VECTOR ( 'NONE', #72907, 1000.000000000000000 ) ;
#129401=EDGE_CURVE ( 'NONE', #125809, #119594, #88299, .T. ) ;
#129402=VECTOR ( 'NONE', #4730, 1000.000000000000227 ) ;
#129404=CARTESIAN_POINT ( 'NONE',  ( 8.999999999999937828, -10.44781430457071991, 5.000000000000000000 ) ) ;
#129405=DIRECTION ( 'NONE',  ( 0.3543493200069162685, -0.000000000000000000, -0.9351131265310288487 ) ) ;
#129406=VECTOR ( 'NONE', #59492, 1000.000000000000000 ) ;
#129407=LINE ( 'NONE', #96058, #44845 ) ;
#129408=LINE ( 'NONE', #110494, #46100 ) ;
#129409=VERTEX_POINT ( 'NONE', #34621 ) ;
#129410=DIRECTION ( 'NONE',  ( 0.7071067811865487940, 0.7071067811865463515, 0.000000000000000000 ) ) ;
#129411=ORIENTED_EDGE ( 'NONE', *, *, #11241, .T. ) ;
#129412=ADVANCED_FACE ( 'NONE', ( #131080 ), #119454, .F. ) ;
#129413=VECTOR ( 'NONE', #62427, 1000.000000000000000 ) ;
#129414=CARTESIAN_POINT ( 'NONE',  ( 13.49999999999990763, -5.947814304570766986, 5.000000000000000000 ) ) ;
#129416=ORIENTED_EDGE ( 'NONE', *, *, #16644, .T. ) ;
#129417=CARTESIAN_POINT ( 'NONE',  ( -26.99451991528749417, 28.92564299267956685, 4.000000000000000000 ) ) ;
#129418=DIRECTION ( 'NONE',  ( 0.7071067811865487940, 0.7071067811865463515, 0.000000000000000000 ) ) ;
#129419=ORIENTED_EDGE ( 'NONE', *, *, #96108, .F. ) ;
#129421=EDGE_CURVE ( 'NONE', #27623, #22382, #53523, .T. ) ;
#129422=CARTESIAN_POINT ( 'NONE',  ( 63.18398860626900415, 28.73617430169831621, 5.000000000000000000 ) ) ;
#129424=CARTESIAN_POINT ( 'NONE',  ( 0.000000000000000000, 0.000000000000000000, 5.000000000000000000 ) ) ;
#129425=VECTOR ( 'NONE', #108008, 1000.000000000000114 ) ;
#129426=AXIS2_PLACEMENT_3D ( 'NONE', #37497, #7504, #62636 ) ;
#129427=CARTESIAN_POINT ( 'NONE',  ( 5.207106781186507050, 9.759292476615614831, 5.000000000000000000 ) ) ;
#129430=DIRECTION ( 'NONE',  ( 0.3543493200069162685, -0.000000000000000000, -0.9351131265310288487 ) ) ;
#129431=ADVANCED_FACE ( 'NONE', ( #32488 ), #10688, .T. ) ;
#129434=LINE ( 'NONE', #139648, #118420 ) ;
#129435=EDGE_CURVE ( 'NONE', #38928, #19893, #76727, .T. ) ;
#129439=LINE ( 'NONE', #4202, #33152 ) ;
#129440=PLANE ( 'NONE',  #47639 ) ;
#129442=VECTOR ( 'NONE', #51061, 1000.000000000000000 ) ;
#129443=VECTOR ( 'NONE', #86681, 1000.000000000000114 ) ;
#129444=EDGE_CURVE ( 'NONE', #76266, #139011, #110714, .T. ) ;
#129446=CARTESIAN_POINT ( 'NONE',  ( -66.18398860626901126, 28.73617430169833753, 5.000000000000000000 ) ) ;
#129447=VERTEX_POINT ( 'NONE', #21606 ) ;
#129448=CARTESIAN_POINT ( 'NONE',  ( 12.48921356237309155, -27.52281430457064104, 5.000000000000000000 ) ) ;
#129449=LINE ( 'NONE', #118572, #90363 ) ;
#129450=DIRECTION ( 'NONE',  ( -0.7071067811865486830, -0.7071067811865464625, -0.000000000000000000 ) ) ;
#129451=VERTEX_POINT ( 'NONE', #65133 ) ;
#129452=ORIENTED_EDGE ( 'NONE', *, *, #26546, .T. ) ;
#129453=DIRECTION ( 'NONE',  ( -0.000000000000000000, 0.3543493200069153248, 0.9351131265310292928 ) ) ;
#129454=VECTOR ( 'NONE', #91835, 1000.000000000000000 ) ;
#129455=AXIS2_PLACEMENT_3D ( 'NONE', #121395, #54743, #77227 ) ;
#129456=CARTESIAN_POINT ( 'NONE',  ( -5.671830600776429421, 11.25929247661560240, 4.000000000000000000 ) ) ;
#129458=CARTESIAN_POINT ( 'NONE',  ( 12.79289321881337038, -20.24070752338407431, 5.000000000000000000 ) ) ;
#129459=PLANE ( 'NONE',  #120087 ) ;
#129460=EDGE_LOOP ( 'NONE', ( #34484, #65658, #47050 ) ) ;
#129461=EDGE_CURVE ( 'NONE', #39821, #50567, #54269, .T. ) ;
#129463=CARTESIAN_POINT ( 'NONE',  ( -14.81601139373099585, 28.73617430169776910, 5.000000000000000000 ) ) ;
#129465=VECTOR ( 'NONE', #56007, 1000.000000000000000 ) ;
#129466=CARTESIAN_POINT ( 'NONE',  ( 20.25795612380215971, -2.670494247963030698, 4.000000000000000000 ) ) ;
#129468=EDGE_CURVE ( 'NONE', #89471, #46947, #78139, .T. ) ;
#129469=DIRECTION ( 'NONE',  ( 0.7071067811865487940, 0.7071067811865463515, 0.000000000000000000 ) ) ;
#129470=VERTEX_POINT ( 'NONE', #44079 ) ;
#129472=DIRECTION ( 'NONE',  ( 0.6830127018922180770, -0.6830127018922204085, -0.2588190451025213501 ) ) ;
#129473=DIRECTION ( 'NONE',  ( 0.3543493200069162685, -0.000000000000000000, -0.9351131265310288487 ) ) ;
#129476=LINE ( 'NONE', #42511, #46588 ) ;
#129477=LINE ( 'NONE', #30169, #115736 ) ;
#129478=DIRECTION ( 'NONE',  ( -0.7071067811865487940, 0.7071067811865463515, -0.000000000000000000 ) ) ;
#129479=ORIENTED_EDGE ( 'NONE', *, *, #7285, .T. ) ;
#129480=LINE ( 'NONE', #95430, #69244 ) ;
#129481=LINE ( 'NONE', #141070, #12897 ) ;
#129482=DIRECTION ( 'NONE',  ( -0.000000000000000000, 0.000000000000000000, 1.000000000000000000 ) ) ;
#129483=FACE_OUTER_BOUND ( 'NONE', #44982, .T. ) ;
#129484=ORIENTED_EDGE ( 'NONE', *, *, #127366, .T. ) ;
#129485=EDGE_CURVE ( 'NONE', #132586, #65489, #132548, .T. ) ;
#129486=ORIENTED_EDGE ( 'NONE', *, *, #1356, .F. ) ;
#129488=VERTEX_POINT ( 'NONE', #121608 ) ;
#129489=CARTESIAN_POINT ( 'NONE',  ( 17.99999999999987566, 19.55218569542897100, 5.000000000000000000 ) ) ;
#129491=CARTESIAN_POINT ( 'NONE',  ( 20.77868544475317947, 8.889383937919465239, 4.212719859983347526 ) ) ;
#129492=LINE ( 'NONE', #110583, #33933 ) ;
#129493=ORIENTED_EDGE ( 'NONE', *, *, #107462, .F. ) ;
#129494=DIRECTION ( 'NONE',  ( 0.6830127018922180770, -0.6830127018922204085, -0.2588190451025213501 ) ) ;
#129495=VERTEX_POINT ( 'NONE', #22276 ) ;
#129498=DIRECTION ( 'NONE',  ( -1.000000000000000000, 0.000000000000000000, 0.000000000000000000 ) ) ;
#129500=AXIS2_PLACEMENT_3D ( 'NONE', #29642, #118056, #19495 ) ;
#129501=EDGE_LOOP ( 'NONE', ( #106337, #52700, #17944, #64448 ) ) ;
#129502=VERTEX_POINT ( 'NONE', #55673 ) ;
#129503=VECTOR ( 'NONE', #69483, 1000.000000000000000 ) ;
#129504=DIRECTION ( 'NONE',  ( -0.000000000000000000, -0.3543493200069152693, 0.9351131265310292928 ) ) ;
#129506=CARTESIAN_POINT ( 'NONE',  ( 12.48921356237309155, -27.52281430457064104, 5.000000000000000000 ) ) ;
#129508=AXIS2_PLACEMENT_3D ( 'NONE', #16567, #28187, #114461 ) ;
#129509=DIRECTION ( 'NONE',  ( -0.7071067811865486830, -0.7071067811865464625, 0.000000000000000000 ) ) ;
#129513=VECTOR ( 'NONE', #126058, 1000.000000000000227 ) ;
#129514=VERTEX_POINT ( 'NONE', #539 ) ;
#129515=VERTEX_POINT ( 'NONE', #44834 ) ;
#129516=VERTEX_POINT ( 'NONE', #89024 ) ;
#129517=VECTOR ( 'NONE', #6361, 1000.000000000000000 ) ;
#129518=VECTOR ( 'NONE', #110382, 999.9999999999998863 ) ;
#129522=DIRECTION ( 'NONE',  ( 0.7071067811865486830, -0.7071067811865464625, -0.000000000000000000 ) ) ;
#129523=VERTEX_POINT ( 'NONE', #22986 ) ;
#129524=CARTESIAN_POINT ( 'NONE',  ( 19.17183060077633883, 15.75929247661555976, 4.000000000000000000 ) ) ;
#129526=LINE ( 'NONE', #73059, #112823 ) ;
#129529=VECTOR ( 'NONE', #97963, 1000.000000000000000 ) ;
#129530=DIRECTION ( 'NONE',  ( 0.7071067811865487940, 0.7071067811865463515, -0.000000000000000000 ) ) ;
#129531=ORIENTED_EDGE ( 'NONE', *, *, #57651, .F. ) ;
#129532=VECTOR ( 'NONE', #114649, 1000.000000000000000 ) ;
#129533=CARTESIAN_POINT ( 'NONE',  ( 17.27718569542927796, -21.72500000000000142, 5.000000000000000000 ) ) ;
#129536=VERTEX_POINT ( 'NONE', #67257 ) ;
#129537=CARTESIAN_POINT ( 'NONE',  ( -48.29974487139158867, -27.71228299555239971, 4.000000000000000000 ) ) ;
#129539=ADVANCED_FACE ( 'NONE', ( #56421 ), #100604, .F. ) ;
#129540=EDGE_CURVE ( 'NONE', #129197, #2861, #123069, .T. ) ;
#129541=FACE_OUTER_BOUND ( 'NONE', #73737, .T. ) ;
#129542=ORIENTED_EDGE ( 'NONE', *, *, #136579, .F. ) ;
#129544=AXIS2_PLACEMENT_3D ( 'NONE', #137340, #72839, #17660 ) ;
#129547=ADVANCED_FACE ( 'NONE', ( #59266 ), #1937, .F. ) ;
#129548=EDGE_CURVE ( 'NONE', #12163, #60612, #137512, .T. ) ;
#129549=LINE ( 'NONE', #139756, #18794 ) ;
#129550=FACE_OUTER_BOUND ( 'NONE', #95557, .T. ) ;
#129551=ADVANCED_FACE ( 'NONE', ( #70155 ), #134672, .F. ) ;
#129553=CARTESIAN_POINT ( 'NONE',  ( -34.42500000000001137, 7.541399257801932876, 5.000000000000000000 ) ) ;
#129554=EDGE_CURVE ( 'NONE', #25495, #131632, #48350, .T. ) ;
#129555=LINE ( 'NONE', #95499, #51355 ) ;
#129556=PLANE ( 'NONE',  #81106 ) ;
#129557=AXIS2_PLACEMENT_3D ( 'NONE', #107691, #9811, #141034 ) ;
#129558=DIRECTION ( 'NONE',  ( -0.7071067811865486830, -0.7071067811865464625, 0.000000000000000000 ) ) ;
#129559=EDGE_CURVE ( 'NONE', #28420, #7787, #78860, .T. ) ;
#129560=FACE_OUTER_BOUND ( 'NONE', #77843, .T. ) ;
#129562=CARTESIAN_POINT ( 'NONE',  ( 48.18398860626899705, 28.73617430169820608, 5.000000000000000000 ) ) ;
#129563=EDGE_CURVE ( 'NONE', #101765, #121732, #76767, .T. ) ;
#129564=ORIENTED_EDGE ( 'NONE', *, *, #138720, .T. ) ;
#129566=ORIENTED_EDGE ( 'NONE', *, *, #68285, .T. ) ;
#129567=EDGE_LOOP ( 'NONE', ( #106596, #1323, #63626, #50909 ) ) ;
#129568=ORIENTED_EDGE ( 'NONE', *, *, #66299, .T. ) ;
#129569=VERTEX_POINT ( 'NONE', #79609 ) ;
#129570=DIRECTION ( 'NONE',  ( -0.7071067811865486830, -0.7071067811865464625, -0.000000000000000000 ) ) ;
#129571=CARTESIAN_POINT ( 'NONE',  ( -54.29974487139159578, -27.71228299555243879, 4.000000000000000000 ) ) ;
#129572=EDGE_CURVE ( 'NONE', #138304, #104351, #112887, .T. ) ;
#129574=VERTEX_POINT ( 'NONE', #92539 ) ;
#129576=VERTEX_POINT ( 'NONE', #113591 ) ;
#129580=CARTESIAN_POINT ( 'NONE',  ( 51.48921356237309510, -27.52281430457091460, 5.000000000000000000 ) ) ;
#129582=EDGE_LOOP ( 'NONE', ( #24269, #132545, #103324, #43126 ) ) ;
#129583=ADVANCED_FACE ( 'NONE', ( #36067 ), #80991, .F. ) ;
#129584=ORIENTED_EDGE ( 'NONE', *, *, #37156, .F. ) ;
#129586=DIRECTION ( 'NONE',  ( 0.7071067811865487940, 0.7071067811865463515, 0.000000000000000000 ) ) ;
#129587=DIRECTION ( 'NONE',  ( 0.7071067811865487940, 0.7071067811865463515, 0.000000000000000000 ) ) ;
#129588=FACE_OUTER_BOUND ( 'NONE', #104563, .T. ) ;
#129589=FACE_OUTER_BOUND ( 'NONE', #39625, .T. ) ;
#129590=ADVANCED_FACE ( 'NONE', ( #58575 ), #80291, .F. ) ;
#129591=FACE_OUTER_BOUND ( 'NONE', #79110, .T. ) ;
#129595=EDGE_CURVE ( 'NONE', #3062, #84892, #49088, .T. ) ;
#129596=ORIENTED_EDGE ( 'NONE', *, *, #116977, .T. ) ;
#129598=AXIS2_PLACEMENT_3D ( 'NONE', #67683, #111870, #56812 ) ;
#129599=AXIS2_PLACEMENT_3D ( 'NONE', #2232, #121184, #134227 ) ;
#129600=CIRCLE ( 'NONE', #67128, 5.968999999999998529 ) ;
#129601=AXIS2_PLACEMENT_3D ( 'NONE', #68833, #2816, #123920 ) ;
#129602=CARTESIAN_POINT ( 'NONE',  ( 33.48921356237309510, -27.52281430457078670, 5.000000000000000000 ) ) ;
#129603=ORIENTED_EDGE ( 'NONE', *, *, #32806, .T. ) ;
#129604=( BOUNDED_CURVE ( )  B_SPLINE_CURVE ( 3, ( #81124, #26719, #4918, #49215 ),
 .UNSPECIFIED., .F., .T. ) 
 B_SPLINE_CURVE_WITH_KNOTS ( ( 4, 4 ),
 ( 3.995629653766860301, 4.163580865291908850 ),
 .UNSPECIFIED. ) 
 CURVE ( )  GEOMETRIC_REPRESENTATION_ITEM ( )  RATIONAL_B_SPLINE_CURVE ( ( 1.000000000000000000, 0.9976507469244630943, 0.9976507469244630943, 1.000000000000000000 ) ) 
 REPRESENTATION_ITEM ( '' )  );
#129605=EDGE_CURVE ( 'NONE', #1952, #27121, #70842, .T. ) ;
#129608=CARTESIAN_POINT ( 'NONE',  ( -6.489213562373093325, -27.52281430457059841, 5.000000000000000000 ) ) ;
#129611=DIRECTION ( 'NONE',  ( -0.7071067811865486830, 0.7071067811865464625, 0.000000000000000000 ) ) ;
#129613=EDGE_LOOP ( 'NONE', ( #139266, #110498, #1475, #42169 ) ) ;
#129614=DIRECTION ( 'NONE',  ( -0.7071067811865486830, -0.7071067811865464625, 0.000000000000000000 ) ) ;
#129615=VECTOR ( 'NONE', #64222, 1000.000000000000000 ) ;
#129616=ORIENTED_EDGE ( 'NONE', *, *, #40070, .T. ) ;
#129617=DIRECTION ( 'NONE',  ( -0.6830127018922181881, 0.6830127018922202975, -0.2588190451025214056 ) ) ;
#129621=EDGE_CURVE ( 'NONE', #133913, #37030, #23746, .T. ) ;
#129622=DIRECTION ( 'NONE',  ( -0.6830127018922180770, -0.6830127018922204085, -0.2588190451025213501 ) ) ;
#129623=CARTESIAN_POINT ( 'NONE',  ( 9.183988606268997046, 28.73617430169793607, 5.000000000000000000 ) ) ;
#129626=VECTOR ( 'NONE', #54440, 1000.000000000000000 ) ;
#129627=VECTOR ( 'NONE', #29854, 999.9999999999998863 ) ;
#129628=CARTESIAN_POINT ( 'NONE',  ( 63.48921356237309510, -27.52281430457099631, 5.000000000000000000 ) ) ;
#129629=DIRECTION ( 'NONE',  ( 0.7071067811865486830, -0.7071067811865464625, -0.000000000000000000 ) ) ;
#129631=ORIENTED_EDGE ( 'NONE', *, *, #11820, .F. ) ;
#129634=ORIENTED_EDGE ( 'NONE', *, *, #31880, .F. ) ;
#129635=EDGE_CURVE ( 'NONE', #38115, #139654, #12841, .T. ) ;
#129636=DIRECTION ( 'NONE',  ( 0.6830127018922180770, -0.6830127018922204085, -0.2588190451025213501 ) ) ;
#129638=DIRECTION ( 'NONE',  ( -0.3543493200069162685, -0.000000000000000000, -0.9351131265310288487 ) ) ;
#129640=ORIENTED_EDGE ( 'NONE', *, *, #90642, .T. ) ;
#129642=DIRECTION ( 'NONE',  ( 0.7071067811865486830, -0.7071067811865464625, -0.000000000000000000 ) ) ;
#129644=CARTESIAN_POINT ( 'NONE',  ( 39.48921356237310221, -27.52281430457082934, 5.000000000000000000 ) ) ;
#129646=AXIS2_PLACEMENT_3D ( 'NONE', #136095, #66575, #90460 ) ;
#129647=LINE ( 'NONE', #7859, #33270 ) ;
#129648=DIRECTION ( 'NONE',  ( 0.7071067811865487940, 0.7071067811865463515, 0.000000000000000000 ) ) ;
#129649=ORIENTED_EDGE ( 'NONE', *, *, #97458, .F. ) ;
#129651=VECTOR ( 'NONE', #138234, 1000.000000000000000 ) ;
#129653=FACE_OUTER_BOUND ( 'NONE', #137291, .T. ) ;
#129654=CARTESIAN_POINT ( 'NONE',  ( -68.99451991528748351, 28.92564299267986172, 4.000000000000000000 ) ) ;
#129655=CARTESIAN_POINT ( 'NONE',  ( 17.99999999999987566, -10.77435723561694125, -9.972017380717273838 ) ) ;
#129656=ORIENTED_EDGE ( 'NONE', *, *, #2911, .F. ) ;
#129657=EDGE_LOOP ( 'NONE', ( #107711, #133558, #60392, #48212 ) ) ;
#129658=ORIENTED_EDGE ( 'NONE', *, *, #139313, .F. ) ;
#129661=EDGE_LOOP ( 'NONE', ( #115103, #102177, #3270, #75454, #117412, #114315 ) ) ;
#129663=VECTOR ( 'NONE', #42301, 1000.000000000000227 ) ;
#129664=CARTESIAN_POINT ( 'NONE',  ( 11.20710678118647152, -20.24070752338407431, 5.000000000000000000 ) ) ;
#129670=EDGE_CURVE ( 'NONE', #91137, #3249, #41044, .T. ) ;
#129671=VERTEX_POINT ( 'NONE', #17153 ) ;
#129672=CARTESIAN_POINT ( 'NONE',  ( 6.489213562373093325, -27.52281430457059841, 5.000000000000000000 ) ) ;
#129673=DIRECTION ( 'NONE',  ( 0.7071067811865487940, 0.7071067811865463515, 0.000000000000000000 ) ) ;
#129674=CARTESIAN_POINT ( 'NONE',  ( 16.49999999999988987, 9.431123077392092213, 4.000000000000000000 ) ) ;
#129675=AXIS2_PLACEMENT_3D ( 'NONE', #57393, #132097, #46545 ) ;
#129676=DIRECTION ( 'NONE',  ( -0.000000000000000000, 0.3543493200069153248, 0.9351131265310292928 ) ) ;
#129677=ORIENTED_EDGE ( 'NONE', *, *, #55938, .T. ) ;
#129678=VERTEX_POINT ( 'NONE', #38205 ) ;
#129679=VERTEX_POINT ( 'NONE', #128761 ) ;
#129680=LINE ( 'NONE', #20191, #44584 ) ;
#129681=ADVANCED_FACE ( 'NONE', ( #40359 ), #60702, .T. ) ;
#129682=DIRECTION ( 'NONE',  ( -0.6830127018922181881, 0.6830127018922202975, -0.2588190451025214056 ) ) ;
#129686=EDGE_LOOP ( 'NONE', ( #124075, #43309, #120756, #42623 ) ) ;
#129687=ORIENTED_EDGE ( 'NONE', *, *, #64760, .F. ) ;
#129688=CARTESIAN_POINT ( 'NONE',  ( 39.48921356237310221, -27.52281430457082934, 5.000000000000000000 ) ) ;
#129689=ORIENTED_EDGE ( 'NONE', *, *, #119384, .T. ) ;
#129690=ORIENTED_EDGE ( 'NONE', *, *, #22626, .F. ) ;
#129691=VECTOR ( 'NONE', #28881, 1000.000000000000000 ) ;
#129694=DIRECTION ( 'NONE',  ( -0.7071067811865486830, -0.7071067811865464625, 0.000000000000000000 ) ) ;
#129695=FACE_OUTER_BOUND ( 'NONE', #102681, .T. ) ;
#129696=ORIENTED_EDGE ( 'NONE', *, *, #70567, .F. ) ;
#129699=EDGE_CURVE ( 'NONE', #106533, #117346, #6223, .T. ) ;
#129700=CARTESIAN_POINT ( 'NONE',  ( -3.280019679894024875, 0.7592924766157104211, 14.27032725228008125 ) ) ;
#129701=CARTESIAN_POINT ( 'NONE',  ( 60.48921356237309510, -27.52281430457097500, 5.000000000000000000 ) ) ;
#129705=ORIENTED_EDGE ( 'NONE', *, *, #91884, .T. ) ;
#129706=VECTOR ( 'NONE', #32413, 1000.000000000000000 ) ;
#129708=CARTESIAN_POINT ( 'NONE',  ( 0.000000000000000000, 0.000000000000000000, 4.000000000000000000 ) ) ;
#129709=VERTEX_POINT ( 'NONE', #82417 ) ;
#129711=DIRECTION ( 'NONE',  ( 0.3543493200069162685, -0.000000000000000000, -0.9351131265310288487 ) ) ;
#129713=EDGE_CURVE ( 'NONE', #73159, #44574, #96119, .T. ) ;
#129714=ORIENTED_EDGE ( 'NONE', *, *, #136019, .T. ) ;
#129715=DIRECTION ( 'NONE',  ( -0.7071067811865486830, -0.7071067811865464625, 0.000000000000000000 ) ) ;
#129716=ORIENTED_EDGE ( 'NONE', *, *, #62506, .T. ) ;
#129717=ORIENTED_EDGE ( 'NONE', *, *, #65306, .T. ) ;
#129720=EDGE_CURVE ( 'NONE', #59677, #43567, #8370, .T. ) ;
#129723=DIRECTION ( 'NONE',  ( 0.7071067811865487940, 0.7071067811865463515, 0.000000000000000000 ) ) ;
#129724=ADVANCED_FACE ( 'NONE', ( #50498 ), #117851, .F. ) ;
#129726=CARTESIAN_POINT ( 'NONE',  ( 6.328169399223481761, -18.74070752338408852, 4.000000000000000000 ) ) ;
#129727=EDGE_CURVE ( 'NONE', #71286, #31203, #138218, .T. ) ;
#129728=LINE ( 'NONE', #106524, #133929 ) ;
#129730=AXIS2_PLACEMENT_3D ( 'NONE', #63707, #63001, #7851 ) ;
#129732=LINE ( 'NONE', #140604, #35409 ) ;
#129733=VECTOR ( 'NONE', #125607, 1000.000000000000000 ) ;
#129734=LINE ( 'NONE', #64488, #122287 ) ;
#129735=VECTOR ( 'NONE', #134941, 1000.000000000000000 ) ;
#129736=CARTESIAN_POINT ( 'NONE',  ( -29.99999999999978684, 13.55218569542902429, 5.000000000000000000 ) ) ;
#129737=DIRECTION ( 'NONE',  ( -0.7071067811865487940, 0.7071067811865463515, -0.000000000000000000 ) ) ;
#129738=EDGE_CURVE ( 'NONE', #132753, #8318, #116031, .T. ) ;
#129739=VERTEX_POINT ( 'NONE', #73003 ) ;
#129740=AXIS2_PLACEMENT_3D ( 'NONE', #46442, #55871, #45715 ) ;
#129741=VERTEX_POINT ( 'NONE', #107003 ) ;
#129742=ORIENTED_EDGE ( 'NONE', *, *, #16485, .F. ) ;
#129745=ORIENTED_EDGE ( 'NONE', *, *, #11960, .F. ) ;
#129747=ORIENTED_EDGE ( 'NONE', *, *, #99694, .F. ) ;
#129748=LINE ( 'NONE', #40621, #116190 ) ;
#129749=DIRECTION ( 'NONE',  ( -0.000000000000000000, 0.000000000000000000, 1.000000000000000000 ) ) ;
#129750=EDGE_CURVE ( 'NONE', #28995, #116794, #6934, .T. ) ;
#129751=EDGE_CURVE ( 'NONE', #83991, #18685, #51221, .T. ) ;
#129753=CARTESIAN_POINT ( 'NONE',  ( -6.299744871391586898, -27.71228299555210484, 4.000000000000000000 ) ) ;
#129754=ORIENTED_EDGE ( 'NONE', *, *, #98178, .F. ) ;
#129755=LINE ( 'NONE', #9367, #141376 ) ;
#129756=ORIENTED_EDGE ( 'NONE', *, *, #7281, .F. ) ;
#129757=EDGE_CURVE ( 'NONE', #4199, #126328, #95416, .T. ) ;
#129758=PLANE ( 'NONE',  #104652 ) ;
#129759=DIRECTION ( 'NONE',  ( -0.7071067811865487940, 0.7071067811865463515, -0.000000000000000000 ) ) ;
#129761=ORIENTED_EDGE ( 'NONE', *, *, #126139, .T. ) ;
#129764=LINE ( 'NONE', #30465, #16598 ) ;
#129765=LINE ( 'NONE', #33361, #11815 ) ;
#129766=ORIENTED_EDGE ( 'NONE', *, *, #76253, .T. ) ;
#129767=VERTEX_POINT ( 'NONE', #130935 ) ;
#129768=DIRECTION ( 'NONE',  ( -0.000000000000000000, 0.000000000000000000, 1.000000000000000000 ) ) ;
#129770=ORIENTED_EDGE ( 'NONE', *, *, #12373, .T. ) ;
#129771=PLANE ( 'NONE',  #4541 ) ;
#129772=CARTESIAN_POINT ( 'NONE',  ( -2.277185695429367662, -21.72499999999999432, 5.000000000000000000 ) ) ;
#129773=FACE_OUTER_BOUND ( 'NONE', #27537, .T. ) ;
#129774=DIRECTION ( 'NONE',  ( -0.6830127018922181881, 0.6830127018922202975, -0.2588190451025214056 ) ) ;
#129777=DIRECTION ( 'NONE',  ( -0.6830127018922180770, -0.6830127018922204085, -0.2588190451025213501 ) ) ;
#129778=CARTESIAN_POINT ( 'NONE',  ( -20.99451991528748707, 28.92564299267952777, 4.000000000000000000 ) ) ;
#129781=ORIENTED_EDGE ( 'NONE', *, *, #99435, .F. ) ;
#129782=CARTESIAN_POINT ( 'NONE',  ( -12.29974487139158512, -27.71228299555214747, 4.000000000000000000 ) ) ;
#129783=VECTOR ( 'NONE', #83416, 999.9999999999998863 ) ;
#129784=DIRECTION ( 'NONE',  ( -0.3543493200069162685, -0.000000000000000000, -0.9351131265310288487 ) ) ;
#129785=ORIENTED_EDGE ( 'NONE', *, *, #91007, .F. ) ;
#129786=PLANE ( 'NONE',  #106498 ) ;
#129787=ORIENTED_EDGE ( 'NONE', *, *, #103126, .T. ) ;
#129788=EDGE_LOOP ( 'NONE', ( #18127, #89274, #13587, #97488 ) ) ;
#129789=LINE ( 'NONE', #141384, #16969 ) ;
#129790=FACE_OUTER_BOUND ( 'NONE', #59340, .T. ) ;
#129794=VECTOR ( 'NONE', #130516, 1000.000000000000000 ) ;
#129795=EDGE_CURVE ( 'NONE', #107648, #58396, #121449, .T. ) ;
#129796=CARTESIAN_POINT ( 'NONE',  ( -8.590119451170131981, -22.22500000000000142, -4.979270689482284240 ) ) ;
#129797=DIRECTION ( 'NONE',  ( 0.7071067811865487940, 0.7071067811865463515, 0.000000000000000000 ) ) ;
#129800=EDGE_CURVE ( 'NONE', #29397, #4732, #120731, .T. ) ;
#129801=CARTESIAN_POINT ( 'NONE',  ( -8.999999999999941380, 2.342191155542440395, -5.001666872980064404 ) ) ;
#129803=PLANE ( 'NONE',  #102125 ) ;
#129804=CARTESIAN_POINT ( 'NONE',  ( 8.282422613574265569, -21.73023691814493219, 5.000000000000000888 ) ) ;
#129805=FACE_OUTER_BOUND ( 'NONE', #111058, .T. ) ;
#129806=LINE ( 'NONE', #77601, #64568 ) ;
#129808=LINE ( 'NONE', #75447, #11754 ) ;
#129809=PLANE ( 'NONE',  #31564 ) ;
#129810=ORIENTED_EDGE ( 'NONE', *, *, #58193, .F. ) ;
#129811=ORIENTED_EDGE ( 'NONE', *, *, #89094, .F. ) ;
#129812=ORIENTED_EDGE ( 'NONE', *, *, #54489, .T. ) ;
#129815=AXIS2_PLACEMENT_3D ( 'NONE', #33622, #66941, #12541 ) ;
#129816=ORIENTED_EDGE ( 'NONE', *, *, #117503, .F. ) ;
#129817=EDGE_LOOP ( 'NONE', ( #139900, #83653, #139943, #98080 ) ) ;
#129820=DIRECTION ( 'NONE',  ( -0.7071067811865486830, -0.7071067811865464625, 0.000000000000000000 ) ) ;
#129824=AXIS2_PLACEMENT_3D ( 'NONE', #116585, #94104, #138345 ) ;
#129825=VECTOR ( 'NONE', #10487, 1000.000000000000000 ) ;
#129827=LINE ( 'NONE', #76912, #69455 ) ;
#129829=CARTESIAN_POINT ( 'NONE',  ( -19.49999999999986500, -10.04351517176479192, -1.623559851933870757 ) ) ;
#129830=DIRECTION ( 'NONE',  ( -0.000000000000000000, -0.3543493200069152693, 0.9351131265310292928 ) ) ;
#129831=DIRECTION ( 'NONE',  ( -0.000000000000000000, 0.000000000000000000, 1.000000000000000000 ) ) ;
#129834=ORIENTED_EDGE ( 'NONE', *, *, #96381, .F. ) ;
#129835=LINE ( 'NONE', #30538, #51120 ) ;
#129836=CARTESIAN_POINT ( 'NONE',  ( -2.999999999999975131, -6.108550654416966097, -3.114665004254973280 ) ) ;
#129837=VECTOR ( 'NONE', #123804, 1000.000000000000000 ) ;
#129838=LINE ( 'NONE', #53726, #130358 ) ;
#129840=DIRECTION ( 'NONE',  ( 0.6830127018922180770, -0.6830127018922204085, -0.2588190451025213501 ) ) ;
#129841=CARTESIAN_POINT ( 'NONE',  ( -36.48921356237310221, -27.52281430457080802, 5.000000000000000000 ) ) ;
#129842=DIRECTION ( 'NONE',  ( 0.3543493200069162685, -0.000000000000000000, -0.9351131265310288487 ) ) ;
#129843=LINE ( 'NONE', #19648, #72362 ) ;
#129844=ORIENTED_EDGE ( 'NONE', *, *, #101061, .T. ) ;
#129845=ORIENTED_EDGE ( 'NONE', *, *, #46790, .F. ) ;
#129847=EDGE_LOOP ( 'NONE', ( #94669, #117822, #124752, #128432 ) ) ;
#129849=CARTESIAN_POINT ( 'NONE',  ( -48.48921356237309510, -27.52281430457089328, 5.000000000000000000 ) ) ;
#129850=AXIS2_PLACEMENT_3D ( 'NONE', #12103, #22249, #68666 ) ;
#129851=CARTESIAN_POINT ( 'NONE',  ( -29.99999999999979039, -13.06887692260767331, 4.000000000000000000 ) ) ;
#129852=FACE_OUTER_BOUND ( 'NONE', #104437, .T. ) ;
#129853=CARTESIAN_POINT ( 'NONE',  ( -22.49999999999984013, -7.533600742197664069, 5.000000000000000000 ) ) ;
#129854=CARTESIAN_POINT ( 'NONE',  ( -2.510786437626908008, -27.52281430457053446, 5.000000000000000000 ) ) ;
#129856=VECTOR ( 'NONE', #54631, 1000.000000000000000 ) ;
#129858=EDGE_CURVE ( 'NONE', #130889, #13355, #64956, .T. ) ;
#129859=EDGE_LOOP ( 'NONE', ( #102803, #51023, #34914, #32846 ) ) ;
#129860=VECTOR ( 'NONE', #17231, 1000.000000000000000 ) ;
#129861=DIRECTION ( 'NONE',  ( 0.7071067811865486830, -0.7071067811865464625, -0.000000000000000000 ) ) ;
#129862=ORIENTED_EDGE ( 'NONE', *, *, #10926, .F. ) ;
#129863=DIRECTION ( 'NONE',  ( -0.000000000000000000, -0.3543493200069152693, 0.9351131265310292928 ) ) ;
#129864=VECTOR ( 'NONE', #34978, 1000.000000000000000 ) ;
#129865=DIRECTION ( 'NONE',  ( 0.7071067811865487940, 0.7071067811865463515, 0.000000000000000000 ) ) ;
#129867=CARTESIAN_POINT ( 'NONE',  ( -14.29289321881336505, -0.7407075233842874695, 5.000000000000000000 ) ) ;
#129868=ORIENTED_EDGE ( 'NONE', *, *, #57047, .F. ) ;
#129870=ORIENTED_EDGE ( 'NONE', *, *, #11969, .F. ) ;
#129871=VECTOR ( 'NONE', #56209, 999.9999999999998863 ) ;
#129872=CARTESIAN_POINT ( 'NONE',  ( 54.29974487139159578, -27.71228299555243879, 4.000000000000000000 ) ) ;
#129873=ADVANCED_FACE ( 'NONE', ( #131633 ), #55506, .T. ) ;
#129875=CARTESIAN_POINT ( 'NONE',  ( -10.49999999999991829, -8.947814304570735899, 5.000000000000000000 ) ) ;
#129876=DIRECTION ( 'NONE',  ( 0.7071067811865487940, 0.7071067811865463515, 0.000000000000000000 ) ) ;
#129877=AXIS2_PLACEMENT_3D ( 'NONE', #94733, #3442, #136117 ) ;
#129880=CARTESIAN_POINT ( 'NONE',  ( -13.49999999999990763, -20.56887692260760758, 4.000000000000000000 ) ) ;
#129881=VERTEX_POINT ( 'NONE', #44660 ) ;
#129882=ORIENTED_EDGE ( 'NONE', *, *, #33473, .F. ) ;
#129884=EDGE_LOOP ( 'NONE', ( #78411, #60208, #6254, #101937 ) ) ;
#129885=AXIS2_PLACEMENT_3D ( 'NONE', #21009, #6520, #50806 ) ;
#129886=ADVANCED_FACE ( 'NONE', ( #54104 ), #141055, .F. ) ;
#129887=LINE ( 'NONE', #30593, #125517 ) ;
#129888=ORIENTED_EDGE ( 'NONE', *, *, #64950, .F. ) ;
#129889=CARTESIAN_POINT ( 'NONE',  ( -18.18398860626898994, 28.73617430169800002, 5.000000000000000000 ) ) ;
#129890=LINE ( 'NONE', #48960, #50566 ) ;
#129892=FACE_BOUND ( 'NONE', #138862, .T. ) ;
#129893=ORIENTED_EDGE ( 'NONE', *, *, #8245, .F. ) ;
#129894=DIRECTION ( 'NONE',  ( 0.6830127018922181881, 0.6830127018922202975, -0.2588190451025214056 ) ) ;
#129895=LINE ( 'NONE', #73393, #46777 ) ;
#129896=LINE ( 'NONE', #119014, #81027 ) ;
#129897=ORIENTED_EDGE ( 'NONE', *, *, #52401, .F. ) ;
#129898=PLANE ( 'NONE',  #119874 ) ;
#129899=ORIENTED_EDGE ( 'NONE', *, *, #73757, .F. ) ;
#129900=ORIENTED_EDGE ( 'NONE', *, *, #75739, .F. ) ;
#129903=ORIENTED_EDGE ( 'NONE', *, *, #89026, .F. ) ;
#129904=EDGE_CURVE ( 'NONE', #1343, #128385, #132372, .T. ) ;
#129907=CARTESIAN_POINT ( 'NONE',  ( 21.29177708983034378, -15.74070752338412760, 19.73771281079102735 ) ) ;
#129908=EDGE_CURVE ( 'NONE', #128301, #66309, #65704, .T. ) ;
#129910=ORIENTED_EDGE ( 'NONE', *, *, #70019, .F. ) ;
#129911=EDGE_CURVE ( 'NONE', #3561, #118497, #9834, .T. ) ;
#129912=DIRECTION ( 'NONE',  ( 0.7071067811865486830, -0.7071067811865464625, -0.000000000000000000 ) ) ;
#129913=FACE_OUTER_BOUND ( 'NONE', #143512, .T. ) ;
#129914=VECTOR ( 'NONE', #139250, 1000.000000000000000 ) ;
#129915=ADVANCED_FACE ( 'NONE', ( #143209 ), #97552, .F. ) ;
#129916=AXIS2_PLACEMENT_3D ( 'NONE', #118495, #127985, #62723 ) ;
#129918=DIRECTION ( 'NONE',  ( -0.7071067811865486830, -0.7071067811865464625, -0.000000000000000000 ) ) ;
#129919=LINE ( 'NONE', #130657, #80681 ) ;
#129920=LINE ( 'NONE', #17568, #85231 ) ;
#129921=DIRECTION ( 'NONE',  ( 0.6830127018922181881, 0.6830127018922202975, -0.2588190451025214056 ) ) ;
#129922=CARTESIAN_POINT ( 'NONE',  ( 0.2997448713915885632, -27.71228299555206220, 4.000000000000000000 ) ) ;
#129923=VERTEX_POINT ( 'NONE', #41760 ) ;
#129924=VECTOR ( 'NONE', #140646, 1000.000000000000000 ) ;
#129925=AXIS2_PLACEMENT_3D ( 'NONE', #87207, #129264, #29951 ) ;
#129927=ORIENTED_EDGE ( 'NONE', *, *, #8309, .F. ) ;
#129929=LINE ( 'NONE', #40101, #49661 ) ;
#129930=CARTESIAN_POINT ( 'NONE',  ( 0.000000000000000000, 0.000000000000000000, 5.000000000000000000 ) ) ;
#129931=EDGE_LOOP ( 'NONE', ( #92719, #82376, #127674, #82392 ) ) ;
#129933=ORIENTED_EDGE ( 'NONE', *, *, #8768, .F. ) ;
#129935=CARTESIAN_POINT ( 'NONE',  ( -26.47599861414532185, 22.03583458319438293, 4.979811245910090278 ) ) ;
#129936=DIRECTION ( 'NONE',  ( -0.7071067811865486830, -0.7071067811865464625, 0.000000000000000000 ) ) ;
#129937=EDGE_CURVE ( 'NONE', #122378, #39664, #33765, .T. ) ;
#129938=ADVANCED_FACE ( 'NONE', ( #130211 ), #56253, .F. ) ;
#129939=CARTESIAN_POINT ( 'NONE',  ( 39.29974487139159578, -27.71228299555233576, 4.000000000000000000 ) ) ;
#129940=ORIENTED_EDGE ( 'NONE', *, *, #113890, .F. ) ;
#129941=AXIS2_PLACEMENT_3D ( 'NONE', #57670, #2510, #121457 ) ;
#129942=CARTESIAN_POINT ( 'NONE',  ( 4.499999999999968914, 16.18958161055402911, -11.56426086740810355 ) ) ;
#129943=EDGE_CURVE ( 'NONE', #2836, #55005, #108391, .T. ) ;
#129944=DIRECTION ( 'NONE',  ( -0.7071067811865486830, -0.7071067811865464625, -0.000000000000000000 ) ) ;
#129947=EDGE_LOOP ( 'NONE', ( #93611, #85895, #42640, #45412 ) ) ;
#129949=VECTOR ( 'NONE', #90302, 1000.000000000000227 ) ;
#129950=FACE_OUTER_BOUND ( 'NONE', #29882, .T. ) ;
#129951=PLANE ( 'NONE',  #44947 ) ;
#129952=EDGE_CURVE ( 'NONE', #142336, #143446, #42503, .T. ) ;
#129955=PLANE ( 'NONE',  #122564 ) ;
#129956=VERTEX_POINT ( 'NONE', #47519 ) ;
#129957=CARTESIAN_POINT ( 'NONE',  ( -22.88901570796818774, -1.420450978533076114, 4.272001239691292085 ) ) ;
#129959=CARTESIAN_POINT ( 'NONE',  ( -1.828169399223511071, -2.240707523384262601, 4.000000000000000000 ) ) ;
#129960=EDGE_LOOP ( 'NONE', ( #102410, #57299, #74695, #114499 ) ) ;
#129961=VECTOR ( 'NONE', #112599, 1000.000000000000000 ) ;
#129962=VECTOR ( 'NONE', #65899, 1000.000000000000000 ) ;
#129963=AXIS2_PLACEMENT_3D ( 'NONE', #34715, #78954, #59347 ) ;
#129966=EDGE_CURVE ( 'NONE', #6240, #115863, #35636, .T. ) ;
#129967=ORIENTED_EDGE ( 'NONE', *, *, #59800, .T. ) ;
#129968=CARTESIAN_POINT ( 'NONE',  ( 1.499999999999994449, -11.56887692260769818, 4.000000000000000000 ) ) ;
#129969=AXIS2_PLACEMENT_3D ( 'NONE', #14284, #23740, #2678 ) ;
#129970=CARTESIAN_POINT ( 'NONE',  ( 0.7175773864256688173, -21.73023691814493219, 5.000000000000000888 ) ) ;
#129972=VERTEX_POINT ( 'NONE', #1768 ) ;
#129973=VECTOR ( 'NONE', #43683, 1000.000000000000000 ) ;
#129974=ORIENTED_EDGE ( 'NONE', *, *, #30439, .F. ) ;
#129975=FACE_OUTER_BOUND ( 'NONE', #58315, .T. ) ;
#129976=LINE ( 'NONE', #52397, #45956 ) ;
#129977=EDGE_CURVE ( 'NONE', #54208, #92653, #69980, .T. ) ;
#129979=CARTESIAN_POINT ( 'NONE',  ( -7.499999999999944045, 6.052185695429099788, 5.000000000000000000 ) ) ;
#129980=CARTESIAN_POINT ( 'NONE',  ( 5.510786437626906675, -27.52281430457051314, 5.000000000000000000 ) ) ;
#129982=EDGE_LOOP ( 'NONE', ( #112851, #86032, #50042, #60474 ) ) ;
#129983=DIRECTION ( 'NONE',  ( -0.6830127018922180770, -0.6830127018922204085, -0.2588190451025213501 ) ) ;
#129984=PLANE ( 'NONE',  #69903 ) ;
#129986=LINE ( 'NONE', #51004, #139702 ) ;
#129988=LINE ( 'NONE', #29940, #108925 ) ;
#129989=ORIENTED_EDGE ( 'NONE', *, *, #119407, .F. ) ;
#129990=LINE ( 'NONE', #139480, #18702 ) ;
#129992=ADVANCED_FACE ( 'NONE', ( #1080 ), #25703, .F. ) ;
#129993=ORIENTED_EDGE ( 'NONE', *, *, #103498, .F. ) ;
#129994=VECTOR ( 'NONE', #74346, 999.9999999999998863 ) ;
#129995=DIRECTION ( 'NONE',  ( -0.7071067811865487940, 0.7071067811865463515, -0.000000000000000000 ) ) ;
#129996=LINE ( 'NONE', #142319, #143403 ) ;
#129997=ORIENTED_EDGE ( 'NONE', *, *, #75247, .T. ) ;
#129998=FACE_OUTER_BOUND ( 'NONE', #89938, .T. ) ;
#130000=FACE_OUTER_BOUND ( 'NONE', #2821, .T. ) ;
#130003=ADVANCED_FACE ( 'NONE', ( #2497 ), #79438, .F. ) ;
#130004=VERTEX_POINT ( 'NONE', #58398 ) ;
#130005=DIRECTION ( 'NONE',  ( 0.7071067811865487940, 0.7071067811865463515, 0.000000000000000000 ) ) ;
#130009=DIRECTION ( 'NONE',  ( 0.7071067811865487940, 0.7071067811865463515, 0.000000000000000000 ) ) ;
#130010=CARTESIAN_POINT ( 'NONE',  ( 23.36654548503486950, 7.297668562427137573, 4.000000000000000000 ) ) ;
#130011=CARTESIAN_POINT ( 'NONE',  ( 11.64065804060707165, 22.22500000000000142, 22.64546854729260161 ) ) ;
#130014=ORIENTED_EDGE ( 'NONE', *, *, #63275, .T. ) ;
#130015=ORIENTED_EDGE ( 'NONE', *, *, #20592, .F. ) ;
#130017=DIRECTION ( 'NONE',  ( -0.000000000000000000, 0.000000000000000000, 1.000000000000000000 ) ) ;
#130018=DIRECTION ( 'NONE',  ( -0.000000000000000000, -0.3543493200069152693, 0.9351131265310292928 ) ) ;
#130020=VERTEX_POINT ( 'NONE', #36578 ) ;
#130021=AXIS2_PLACEMENT_3D ( 'NONE', #9022, #51169, #119250 ) ;
#130023=( BOUNDED_CURVE ( )  B_SPLINE_CURVE ( 3, ( #85574, #120317, #131239, #42825 ),
 .UNSPECIFIED., .F., .F. ) 
 B_SPLINE_CURVE_WITH_KNOTS ( ( 4, 4 ),
 ( 1.864375635226932504, 1.933014472006540752 ),
 .UNSPECIFIED. ) 
 CURVE ( )  GEOMETRIC_REPRESENTATION_ITEM ( )  RATIONAL_B_SPLINE_CURVE ( ( 1.000000000000000000, 0.9996074310407765395, 0.9996074310407765395, 1.000000000000000000 ) ) 
 REPRESENTATION_ITEM ( '' )  );
#130024=PLANE ( 'NONE',  #111708 ) ;
#130025=VECTOR ( 'NONE', #97253, 999.9999999999998863 ) ;
#130029=VERTEX_POINT ( 'NONE', #35910 ) ;
#130030=LINE ( 'NONE', #43036, #8524 ) ;
#130033=ORIENTED_EDGE ( 'NONE', *, *, #107919, .T. ) ;
#130034=AXIS2_PLACEMENT_3D ( 'NONE', #86154, #84041, #7848 ) ;
#130035=VECTOR ( 'NONE', #99855, 1000.000000000000000 ) ;
#130036=VECTOR ( 'NONE', #3425, 999.9999999999998863 ) ;
#130038=VECTOR ( 'NONE', #139724, 1000.000000000000000 ) ;
#130039=CARTESIAN_POINT ( 'NONE',  ( 34.92499999999998295, 22.22500000000000142, 4.500000000000000888 ) ) ;
#130040=CARTESIAN_POINT ( 'NONE',  ( -33.48921356237309510, -27.52281430457078670, 5.000000000000000000 ) ) ;
#130041=ORIENTED_EDGE ( 'NONE', *, *, #46206, .F. ) ;
#130042=EDGE_CURVE ( 'NONE', #122443, #99871, #78675, .T. ) ;
#130043=DIRECTION ( 'NONE',  ( 1.000000000000000000, 0.000000000000000000, 0.000000000000000000 ) ) ;
#130044=LINE ( 'NONE', #74234, #32707 ) ;
#130046=ORIENTED_EDGE ( 'NONE', *, *, #45995, .F. ) ;
#130048=ADVANCED_FACE ( 'NONE', ( #69235 ), #125020, .T. ) ;
#130049=DIRECTION ( 'NONE',  ( -0.3543493200069162685, -0.000000000000000000, -0.9351131265310288487 ) ) ;
#130050=CARTESIAN_POINT ( 'NONE',  ( -30.79289321881324071, -2.240707523384262601, 5.000000000000000000 ) ) ;
#130051=CARTESIAN_POINT ( 'NONE',  ( -11.99999999999991296, -19.06887692260762179, 4.000000000000000000 ) ) ;
#130053=CARTESIAN_POINT ( 'NONE',  ( 1.734723475976807094E-15, -9.033600742197645417, 5.000000000000000000 ) ) ;
#130055=ADVANCED_FACE ( 'NONE', ( #24288 ), #81555, .F. ) ;
#130058=FACE_OUTER_BOUND ( 'NONE', #76611, .T. ) ;
#130059=DIRECTION ( 'NONE',  ( 0.7071067811865487940, 0.7071067811865463515, 0.000000000000000000 ) ) ;
#130060=CARTESIAN_POINT ( 'NONE',  ( 8.207106781186489286, 9.759292476615614831, 5.000000000000000000 ) ) ;
#130061=VERTEX_POINT ( 'NONE', #100431 ) ;
#130062=ORIENTED_EDGE ( 'NONE', *, *, #142889, .F. ) ;
#130063=FACE_OUTER_BOUND ( 'NONE', #122058, .T. ) ;
#130064=DIRECTION ( 'NONE',  ( 0.7071067811865486830, -0.7071067811865464625, -0.000000000000000000 ) ) ;
#130065=ORIENTED_EDGE ( 'NONE', *, *, #101234, .F. ) ;
#130066=EDGE_CURVE ( 'NONE', #35104, #17758, #3230, .T. ) ;
#130067=VECTOR ( 'NONE', #100128, 1000.000000000000227 ) ;
#130068=ORIENTED_EDGE ( 'NONE', *, *, #37538, .T. ) ;
#130069=AXIS2_PLACEMENT_3D ( 'NONE', #39504, #29309, #127193 ) ;
#130070=CARTESIAN_POINT ( 'NONE',  ( -8.999999999999937828, 7.588810512006198827, -3.013526669885207898 ) ) ;
#130071=VERTEX_POINT ( 'NONE', #89539 ) ;
#130072=VECTOR ( 'NONE', #38646, 1000.000000000000000 ) ;
#130073=CARTESIAN_POINT ( 'NONE',  ( 13.10332671766740020, 3.690788593506699300, 4.000000000000000000 ) ) ;
#130074=CARTESIAN_POINT ( 'NONE',  ( 27.48921356237309155, -27.52281430457074762, 5.000000000000000000 ) ) ;
#130075=AXIS2_PLACEMENT_3D ( 'NONE', #24445, #57823, #76353 ) ;
#130076=LINE ( 'NONE', #30774, #90536 ) ;
#130077=FACE_BOUND ( 'NONE', #68611, .T. ) ;
#130079=DIRECTION ( 'NONE',  ( 0.7071067811865487940, -0.7071067811865463515, 0.000000000000000000 ) ) ;
#130080=CARTESIAN_POINT ( 'NONE',  ( -34.49999999999975131, -4.535744391599457082, 4.994342998332168548 ) ) ;
#130081=CARTESIAN_POINT ( 'NONE',  ( 30.79289321881325137, -8.240707523384195099, 5.000000000000000000 ) ) ;
#130083=DIRECTION ( 'NONE',  ( -0.7071067811865487940, 0.7071067811865463515, 0.000000000000000000 ) ) ;
#130085=ORIENTED_EDGE ( 'NONE', *, *, #87878, .T. ) ;
#130086=EDGE_CURVE ( 'NONE', #93963, #117180, #90998, .T. ) ;
#130087=ORIENTED_EDGE ( 'NONE', *, *, #134937, .F. ) ;
#130089=ORIENTED_EDGE ( 'NONE', *, *, #11156, .F. ) ;
#130090=CARTESIAN_POINT ( 'NONE',  ( -2.999999999999981792, -11.35517001088072853, -1.126524801160114109 ) ) ;
#130091=CARTESIAN_POINT ( 'NONE',  ( 12.32816939922344979, -3.740707523384244837, 4.000000000000000000 ) ) ;
#130092=ADVANCED_FACE ( 'NONE', ( #59103 ), #90247, .F. ) ;
#130093=VECTOR ( 'NONE', #136101, 1000.000000000000000 ) ;
#130094=VERTEX_POINT ( 'NONE', #3908 ) ;
#130096=VECTOR ( 'NONE', #63859, 1000.000000000000000 ) ;
#130097=EDGE_CURVE ( 'NONE', #48100, #99232, #68535, .T. ) ;
#130098=EDGE_CURVE ( 'NONE', #127446, #27313, #135222, .T. ) ;
#130099=LINE ( 'NONE', #32952, #3093 ) ;
#130100=CARTESIAN_POINT ( 'NONE',  ( 5.999999999999959144, -15.03360074219758324, 5.000000000000000000 ) ) ;
#130101=CARTESIAN_POINT ( 'NONE',  ( 2.207106781186531475, -14.24070752338414358, 5.000000000000000000 ) ) ;
#130102=PLANE ( 'NONE',  #99154 ) ;
#130103=PLANE ( 'NONE',  #77444 ) ;
#130104=CARTESIAN_POINT ( 'NONE',  ( 1.499999999999992673, 21.05218569542895679, 5.000000000000000000 ) ) ;
#130105=DIRECTION ( 'NONE',  ( 0.6830127018922180770, -0.6830127018922204085, -0.2588190451025213501 ) ) ;
#130106=ORIENTED_EDGE ( 'NONE', *, *, #64477, .T. ) ;
#130107=VECTOR ( 'NONE', #137279, 1000.000000000000000 ) ;
#130109=ORIENTED_EDGE ( 'NONE', *, *, #39764, .F. ) ;
#130113=EDGE_LOOP ( 'NONE', ( #132660, #102739, #80809, #37925 ) ) ;
#130114=EDGE_CURVE ( 'NONE', #88778, #64888, #24978, .T. ) ;
#130116=ORIENTED_EDGE ( 'NONE', *, *, #53574, .T. ) ;
#130118=AXIS2_PLACEMENT_3D ( 'NONE', #126597, #137507, #71540 ) ;
#130123=EDGE_CURVE ( 'NONE', #44265, #125649, #85084, .T. ) ;
#130124=ORIENTED_EDGE ( 'NONE', *, *, #69041, .T. ) ;
#130125=LINE ( 'NONE', #73599, #101317 ) ;
#130126=ORIENTED_EDGE ( 'NONE', *, *, #27004, .T. ) ;
#130127=LINE ( 'NONE', #118512, #51094 ) ;
#130128=LINE ( 'NONE', #30828, #52139 ) ;
#130129=VECTOR ( 'NONE', #105356, 999.9999999999998863 ) ;
#130130=EDGE_CURVE ( 'NONE', #24067, #117097, #116286, .T. ) ;
#130131=AXIS2_PLACEMENT_3D ( 'NONE', #130677, #33511, #100176 ) ;
#130132=DIRECTION ( 'NONE',  ( -0.7071067811865487940, 0.7071067811865463515, -0.000000000000000000 ) ) ;
#130133=EDGE_LOOP ( 'NONE', ( #29599, #99151, #69778, #68712 ) ) ;
#130134=VECTOR ( 'NONE', #18035, 1000.000000000000000 ) ;
#130135=ORIENTED_EDGE ( 'NONE', *, *, #98030, .F. ) ;
#130136=CARTESIAN_POINT ( 'NONE',  ( -31.49999999999977973, 6.431123077392124188, 4.000000000000000000 ) ) ;
#130137=VECTOR ( 'NONE', #64675, 1000.000000000000227 ) ;
#130138=LINE ( 'NONE', #43832, #100366 ) ;
#130139=AXIS2_PLACEMENT_3D ( 'NONE', #72722, #116874, #97986 ) ;
#130142=VERTEX_POINT ( 'NONE', #138050 ) ;
#130144=VERTEX_POINT ( 'NONE', #51045 ) ;
#130145=LINE ( 'NONE', #142449, #5466 ) ;
#130147=EDGE_CURVE ( 'NONE', #9910, #83102, #27849, .T. ) ;
#130148=VECTOR ( 'NONE', #133916, 1000.000000000000000 ) ;
#130149=PLANE ( 'NONE',  #106318 ) ;
#130150=CARTESIAN_POINT ( 'NONE',  ( -3.183988606268992161, 28.73617430169789699, 5.000000000000000000 ) ) ;
#130151=CARTESIAN_POINT ( 'NONE',  ( -1.410090645198307291, 9.759292476615618384, 11.28811694763778561 ) ) ;
#130152=LINE ( 'NONE', #75073, #74933 ) ;
#130153=CARTESIAN_POINT ( 'NONE',  ( -34.75611968250421313, 19.70565069852387197, 4.955485411084898040 ) ) ;
#130155=CARTESIAN_POINT ( 'NONE',  ( -5.292893218813413903, -12.74070752338415247, 5.000000000000000000 ) ) ;
#130156=VERTEX_POINT ( 'NONE', #4600 ) ;
#130158=DIRECTION ( 'NONE',  ( 0.7071067811865487940, 0.7071067811865463515, -0.000000000000000000 ) ) ;
#130161=EDGE_LOOP ( 'NONE', ( #126705, #367, #109189, #104153 ) ) ;
#130162=CARTESIAN_POINT ( 'NONE',  ( -36.18398860626899705, 28.73617430169812437, 5.000000000000000000 ) ) ;
#130163=FACE_OUTER_BOUND ( 'NONE', #64201, .T. ) ;
#130164=ORIENTED_EDGE ( 'NONE', *, *, #103369, .T. ) ;
#130169=CARTESIAN_POINT ( 'NONE',  ( 48.48921356237309510, -27.52281430457089328, 5.000000000000000000 ) ) ;
#130170=EDGE_CURVE ( 'NONE', #143133, #112059, #6762, .T. ) ;
#130172=VECTOR ( 'NONE', #115771, 1000.000000000000000 ) ;
#130173=LINE ( 'NONE', #75097, #104269 ) ;
#130175=LINE ( 'NONE', #40326, #41383 ) ;
#130176=FACE_OUTER_BOUND ( 'NONE', #125181, .T. ) ;
#130178=VECTOR ( 'NONE', #70266, 1000.000000000000000 ) ;
#130179=VERTEX_POINT ( 'NONE', #106821 ) ;
#130180=CARTESIAN_POINT ( 'NONE',  ( 32.99451991528749062, 28.92564299267960948, 4.000000000000000000 ) ) ;
#130182=CARTESIAN_POINT ( 'NONE',  ( -42.29974487139158157, -27.71228299555235708, 4.000000000000000000 ) ) ;
#130183=DIRECTION ( 'NONE',  ( -0.6830127018922180770, -0.6830127018922204085, -0.2588190451025213501 ) ) ;
#130185=EDGE_LOOP ( 'NONE', ( #120788, #29079, #40109, #138934 ) ) ;
#130187=DIRECTION ( 'NONE',  ( 0.7071067811865487940, 0.7071067811865463515, 0.000000000000000000 ) ) ;
#130190=CARTESIAN_POINT ( 'NONE',  ( 34.92499999999998295, -21.18334561358932433, 4.500000000000000888 ) ) ;
#130191=LINE ( 'NONE', #109844, #72707 ) ;
#130193=EDGE_LOOP ( 'NONE', ( #115912, #66091, #114835, #100194 ) ) ;
#130194=DIRECTION ( 'NONE',  ( 0.7071067811865487940, -0.7071067811865463515, 0.000000000000000000 ) ) ;
#130195=DIRECTION ( 'NONE',  ( -0.000000000000000000, 0.3543493200069153248, 0.9351131265310292928 ) ) ;
#130198=DIRECTION ( 'NONE',  ( -0.7071067811865486830, -0.7071067811865464625, -0.000000000000000000 ) ) ;
#130200=LINE ( 'NONE', #118583, #55553 ) ;
#130201=DIRECTION ( 'NONE',  ( -0.3543493200069162685, -0.000000000000000000, -0.9351131265310288487 ) ) ;
#130202=ORIENTED_EDGE ( 'NONE', *, *, #38945, .F. ) ;
#130203=( BOUNDED_CURVE ( )  B_SPLINE_CURVE ( 3, ( #83421, #38481, #94971, #116012 ),
 .UNSPECIFIED., .F., .T. ) 
 B_SPLINE_CURVE_WITH_KNOTS ( ( 4, 4 ),
 ( 5.920967161967927161, 7.341195215986599187 ),
 .UNSPECIFIED. ) 
 CURVE ( )  GEOMETRIC_REPRESENTATION_ITEM ( )  RATIONAL_B_SPLINE_CURVE ( ( 1.000000000000000000, 0.8388583629366698213, 0.8388583629366698213, 1.000000000000000000 ) ) 
 REPRESENTATION_ITEM ( '' )  );
#130204=DIRECTION ( 'NONE',  ( 0.7071067811865487940, 0.7071067811865463515, -0.000000000000000000 ) ) ;
#130205=EDGE_CURVE ( 'NONE', #107763, #118405, #50330, .T. ) ;
#130206=CARTESIAN_POINT ( 'NONE',  ( 12.39635797468499590, -22.22500000000000142, -12.93183150186171027 ) ) ;
#130208=AXIS2_PLACEMENT_3D ( 'NONE', #82992, #115562, #62670 ) ;
#130210=ORIENTED_EDGE ( 'NONE', *, *, #68484, .F. ) ;
#130211=FACE_OUTER_BOUND ( 'NONE', #124098, .T. ) ;
#130212=ORIENTED_EDGE ( 'NONE', *, *, #2155, .T. ) ;
#130215=LINE ( 'NONE', #73680, #44802 ) ;
#130216=AXIS2_PLACEMENT_3D ( 'NONE', #131945, #32634, #99265 ) ;
#130217=ORIENTED_EDGE ( 'NONE', *, *, #40337, .T. ) ;
#130218=VECTOR ( 'NONE', #10043, 1000.000000000000000 ) ;
#130219=PLANE ( 'NONE',  #97466 ) ;
#130220=CARTESIAN_POINT ( 'NONE',  ( 14.51078643762690490, -27.52281430457045275, 5.000000000000000000 ) ) ;
#130221=CARTESIAN_POINT ( 'NONE',  ( -41.99451991528749062, 28.92564299267967343, 4.000000000000000000 ) ) ;
#130222=ADVANCED_FACE ( 'NONE', ( #17665 ), #139511, .F. ) ;
#130223=CARTESIAN_POINT ( 'NONE',  ( -11.20710678118646442, -5.240707523384228850, 5.000000000000000000 ) ) ;
#130224=CARTESIAN_POINT ( 'NONE',  ( -14.58437909282842249, -0.7858193515946169105, 4.111732654926457009 ) ) ;
#130225=ORIENTED_EDGE ( 'NONE', *, *, #67773, .F. ) ;
#130226=ADVANCED_FACE ( 'NONE', ( #82261 ), #104693, .F. ) ;
#130228=LINE ( 'NONE', #30917, #26784 ) ;
#130229=VECTOR ( 'NONE', #7321, 1000.000000000000000 ) ;
#130230=( BOUNDED_CURVE ( )  B_SPLINE_CURVE ( 3, ( #50013, #26112, #36968, #139169 ),
 .UNSPECIFIED., .F., .T. ) 
 B_SPLINE_CURVE_WITH_KNOTS ( ( 4, 4 ),
 ( 1.864375635226925398, 1.933014472006533868 ),
 .UNSPECIFIED. ) 
 CURVE ( )  GEOMETRIC_REPRESENTATION_ITEM ( )  RATIONAL_B_SPLINE_CURVE ( ( 1.000000000000000000, 0.9996074310407765395, 0.9996074310407765395, 1.000000000000000000 ) ) 
 REPRESENTATION_ITEM ( '' )  );
#130232=EDGE_CURVE ( 'NONE', #117708, #2398, #51766, .T. ) ;
#130233=ORIENTED_EDGE ( 'NONE', *, *, #119531, .T. ) ;
#130234=ORIENTED_EDGE ( 'NONE', *, *, #121360, .F. ) ;
#130236=ORIENTED_EDGE ( 'NONE', *, *, #20453, .T. ) ;
#130237=ADVANCED_FACE ( 'NONE', ( #84402 ), #117676, .F. ) ;
#130239=DIRECTION ( 'NONE',  ( -0.000000000000000000, -0.3543493200069152693, 0.9351131265310292928 ) ) ;
#130240=DIRECTION ( 'NONE',  ( -0.7071067811865486830, -0.7071067811865464625, 0.000000000000000000 ) ) ;
#130241=DIRECTION ( 'NONE',  ( -0.3543493200069162685, -0.000000000000000000, -0.9351131265310288487 ) ) ;
#130242=ORIENTED_EDGE ( 'NONE', *, *, #13438, .F. ) ;
#130243=VECTOR ( 'NONE', #45643, 999.9999999999998863 ) ;
#130244=AXIS2_PLACEMENT_3D ( 'NONE', #47035, #59311, #136111 ) ;
#130245=LINE ( 'NONE', #64992, #95498 ) ;
#130246=LINE ( 'NONE', #22156, #23542 ) ;
#130248=ADVANCED_FACE ( 'NONE', ( #94516 ), #39465, .T. ) ;
#130250=ORIENTED_EDGE ( 'NONE', *, *, #7836, .T. ) ;
#130251=CARTESIAN_POINT ( 'NONE',  ( -18.24525979340076276, 9.091288135747575438, 4.682346157478786353 ) ) ;
#130252=AXIS2_PLACEMENT_3D ( 'NONE', #75485, #21079, #85614 ) ;
#130253=LINE ( 'NONE', #74445, #128904 ) ;
#130254=CARTESIAN_POINT ( 'NONE',  ( 34.49999999999976552, 0.05432934483094861711, 4.994342998332161443 ) ) ;
#130255=AXIS2_PLACEMENT_3D ( 'NONE', #24803, #4410, #81366 ) ;
#130256=ADVANCED_FACE ( 'NONE', ( #44474 ), #64774, .T. ) ;
#130257=ORIENTED_EDGE ( 'NONE', *, *, #110437, .T. ) ;
#130258=ORIENTED_EDGE ( 'NONE', *, *, #2060, .T. ) ;
#130259=PLANE ( 'NONE',  #52307 ) ;
#130260=DIRECTION ( 'NONE',  ( -0.7071067811865486830, 0.7071067811865464625, 0.000000000000000000 ) ) ;
#130261=FACE_OUTER_BOUND ( 'NONE', #66059, .T. ) ;
#130262=DIRECTION ( 'NONE',  ( -0.3543493200069163240, -0.000000000000000000, 0.9351131265310288487 ) ) ;
#130263=EDGE_CURVE ( 'NONE', #89689, #26788, #21965, .T. ) ;
#130264=EDGE_CURVE ( 'NONE', #36236, #12429, #53155, .T. ) ;
#130265=CARTESIAN_POINT ( 'NONE',  ( -23.20710678118637915, -2.240707523384254163, 5.000000000000000000 ) ) ;
#130266=FACE_OUTER_BOUND ( 'NONE', #58192, .T. ) ;
#130267=ORIENTED_EDGE ( 'NONE', *, *, #87523, .F. ) ;
#130269=ORIENTED_EDGE ( 'NONE', *, *, #83510, .F. ) ;
#130270=EDGE_LOOP ( 'NONE', ( #97479, #86895, #113539, #40576 ) ) ;
#130271=ORIENTED_EDGE ( 'NONE', *, *, #42451, .T. ) ;
#130272=EDGE_CURVE ( 'NONE', #80773, #71223, #107546, .T. ) ;
#130274=AXIS2_PLACEMENT_3D ( 'NONE', #18434, #81625, #28663 ) ;
#130275=CARTESIAN_POINT ( 'NONE',  ( -7.499999999999944045, 4.466399257802216027, 5.000000000000000000 ) ) ;
#130276=EDGE_CURVE ( 'NONE', #13057, #126336, #32881, .T. ) ;
#130277=ADVANCED_FACE ( 'NONE', ( #74961 ), #10364, .T. ) ;
#130278=DIRECTION ( 'NONE',  ( 0.000000000000000000, 0.3543493200069153248, 0.9351131265310291818 ) ) ;
#130279=ORIENTED_EDGE ( 'NONE', *, *, #105019, .T. ) ;
#130280=CARTESIAN_POINT ( 'NONE',  ( 1.499999999999990896, -17.56887692260763956, 4.000000000000000000 ) ) ;
#130281=DIRECTION ( 'NONE',  ( -0.7071067811865486830, -0.7071067811865464625, 0.000000000000000000 ) ) ;
#130285=AXIS2_PLACEMENT_3D ( 'NONE', #60525, #96642, #16991 ) ;
#130287=CARTESIAN_POINT ( 'NONE',  ( -56.99451991528749062, 28.92564299267978001, 4.000000000000000000 ) ) ;
#130288=ORIENTED_EDGE ( 'NONE', *, *, #139627, .T. ) ;
#130289=EDGE_CURVE ( 'NONE', #86768, #116904, #77796, .T. ) ;
#130290=CARTESIAN_POINT ( 'NONE',  ( 15.79289321881334907, 15.75929247661555443, 5.000000000000000000 ) ) ;
#130292=ORIENTED_EDGE ( 'NONE', *, *, #47915, .T. ) ;
#130293=PLANE ( 'NONE',  #41248 ) ;
#130294=ORIENTED_EDGE ( 'NONE', *, *, #36511, .T. ) ;
#130296=ORIENTED_EDGE ( 'NONE', *, *, #1188, .F. ) ;
#130297=ORIENTED_EDGE ( 'NONE', *, *, #10569, .T. ) ;
#130299=ORIENTED_EDGE ( 'NONE', *, *, #89395, .F. ) ;
#130300=ORIENTED_EDGE ( 'NONE', *, *, #124518, .F. ) ;
#130303=CARTESIAN_POINT ( 'NONE',  ( 31.11017322888190151, -22.22500000000000497, 4.785647885939355639 ) ) ;
#130304=EDGE_CURVE ( 'NONE', #29361, #109641, #55330, .T. ) ;
#130305=VECTOR ( 'NONE', #90109, 1000.000000000000000 ) ;
#130306=LINE ( 'NONE', #42595, #79008 ) ;
#130307=ORIENTED_EDGE ( 'NONE', *, *, #25019, .F. ) ;
#130310=EDGE_CURVE ( 'NONE', #39023, #37409, #95452, .T. ) ;
#130311=CARTESIAN_POINT ( 'NONE',  ( 22.82816939922335919, -14.24070752338414714, 4.000000000000000000 ) ) ;
#130312=CARTESIAN_POINT ( 'NONE',  ( -14.81601139373099585, 28.73617430169776910, 5.000000000000000000 ) ) ;
#130314=ORIENTED_EDGE ( 'NONE', *, *, #63495, .T. ) ;
#130315=VERTEX_POINT ( 'NONE', #143039 ) ;
#130316=EDGE_LOOP ( 'NONE', ( #80710, #97728, #103159, #72800 ) ) ;
#130317=ORIENTED_EDGE ( 'NONE', *, *, #53495, .T. ) ;
#130319=AXIS2_PLACEMENT_3D ( 'NONE', #5576, #94718, #117879 ) ;
#130320=ORIENTED_EDGE ( 'NONE', *, *, #55759, .T. ) ;
#130321=CARTESIAN_POINT ( 'NONE',  ( 0.1839886062690032631, 28.73617430169787568, 5.000000000000000000 ) ) ;
#130322=DIRECTION ( 'NONE',  ( -0.6830127018922180770, -0.6830127018922204085, -0.2588190451025213501 ) ) ;
#130323=FACE_OUTER_BOUND ( 'NONE', #80335, .T. ) ;
#130324=ORIENTED_EDGE ( 'NONE', *, *, #86590, .T. ) ;
#130325=VECTOR ( 'NONE', #4246, 1000.000000000000000 ) ;
#130326=ORIENTED_EDGE ( 'NONE', *, *, #11165, .F. ) ;
#130329=PLANE ( 'NONE',  #108463 ) ;
#130331=EDGE_LOOP ( 'NONE', ( #96907, #99817, #20943, #36609 ) ) ;
#130332=VERTEX_POINT ( 'NONE', #8205 ) ;
#130333=VERTEX_POINT ( 'NONE', #97360 ) ;
#130334=LINE ( 'NONE', #74533, #26410 ) ;
#130335=LINE ( 'NONE', #109276, #101987 ) ;
#130336=VECTOR ( 'NONE', #45833, 1000.000000000000000 ) ;
#130337=CARTESIAN_POINT ( 'NONE',  ( -8.999999999999932498, -8.151047557385073361, -8.977947279169777417 ) ) ;
#130338=CARTESIAN_POINT ( 'NONE',  ( -24.79289321881328689, -17.24070752338410628, 5.000000000000000000 ) ) ;
#130340=AXIS2_PLACEMENT_3D ( 'NONE', #83768, #28661, #27197 ) ;
#130341=DIRECTION ( 'NONE',  ( 0.7071067811865487940, 0.7071067811865463515, 0.000000000000000000 ) ) ;
#130345=VERTEX_POINT ( 'NONE', #108224 ) ;
#130346=DIRECTION ( 'NONE',  ( 0.7071067811865487940, 0.7071067811865463515, -0.000000000000000000 ) ) ;
#130347=AXIS2_PLACEMENT_3D ( 'NONE', #116578, #15781, #62940 ) ;
#130348=AXIS2_PLACEMENT_3D ( 'NONE', #137877, #104504, #126270 ) ;
#130351=VERTEX_POINT ( 'NONE', #96634 ) ;
#130352=LINE ( 'NONE', #7819, #32079 ) ;
#130353=DIRECTION ( 'NONE',  ( -0.6830127018922181881, 0.6830127018922202975, -0.2588190451025214056 ) ) ;
#130356=ORIENTED_EDGE ( 'NONE', *, *, #56437, .T. ) ;
#130358=VECTOR ( 'NONE', #19643, 1000.000000000000000 ) ;
#130359=ORIENTED_EDGE ( 'NONE', *, *, #36259, .F. ) ;
#130360=CARTESIAN_POINT ( 'NONE',  ( 30.32816939922330945, -6.740707523384223521, 4.000000000000000000 ) ) ;
#130362=EDGE_LOOP ( 'NONE', ( #139588, #26898, #140009, #8774 ) ) ;
#130365=PLANE ( 'NONE',  #34648 ) ;
#130366=VECTOR ( 'NONE', #107508, 1000.000000000000000 ) ;
#130367=DIRECTION ( 'NONE',  ( 0.7071067811865487940, 0.7071067811865463515, 0.000000000000000000 ) ) ;
#130369=LINE ( 'NONE', #41930, #42526 ) ;
#130370=CARTESIAN_POINT ( 'NONE',  ( -24.79289321881328334, -11.24070752338417556, 5.000000000000000000 ) ) ;
#130373=LINE ( 'NONE', #39813, #44415 ) ;
#130374=DIRECTION ( 'NONE',  ( -0.6830127018922181881, 0.6830127018922202975, -0.2588190451025214056 ) ) ;
#130375=ORIENTED_EDGE ( 'NONE', *, *, #28708, .T. ) ;
#130376=VECTOR ( 'NONE', #96204, 1000.000000000000000 ) ;
#130377=VERTEX_POINT ( 'NONE', #20515 ) ;
#130378=DIRECTION ( 'NONE',  ( -0.000000000000000000, 0.3543493200069153248, 0.9351131265310292928 ) ) ;
#130379=ORIENTED_EDGE ( 'NONE', *, *, #130170, .F. ) ;
#130380=VECTOR ( 'NONE', #59735, 1000.000000000000227 ) ;
#130381=ADVANCED_FACE ( 'NONE', ( #140872 ), #130024, .F. ) ;
#130383=CARTESIAN_POINT ( 'NONE',  ( 0.2997448713915885632, -27.71228299555206220, 4.000000000000000000 ) ) ;
#130385=ORIENTED_EDGE ( 'NONE', *, *, #38549, .F. ) ;
#130386=CARTESIAN_POINT ( 'NONE',  ( 17.99999999999987566, -6.033600742197667621, 5.000000000000000000 ) ) ;
#130387=EDGE_CURVE ( 'NONE', #54291, #31488, #8887, .T. ) ;
#130388=CARTESIAN_POINT ( 'NONE',  ( -57.18398860626899705, 28.73617430169827358, 5.000000000000000000 ) ) ;
#130389=EDGE_CURVE ( 'NONE', #122295, #52699, #66210, .T. ) ;
#130390=EDGE_CURVE ( 'NONE', #98689, #49293, #66949, .T. ) ;
#130392=DIRECTION ( 'NONE',  ( -0.6830127018922180770, -0.6830127018922204085, -0.2588190451025213501 ) ) ;
#130393=ORIENTED_EDGE ( 'NONE', *, *, #125978, .T. ) ;
#130394=CARTESIAN_POINT ( 'NONE',  ( 28.82816939922332722, 0.7592924766157104211, 4.000000000000000000 ) ) ;
#130397=CARTESIAN_POINT ( 'NONE',  ( 81.48921356237309510, -27.52281430457112066, 5.000000000000000000 ) ) ;
#130399=AXIS2_PLACEMENT_3D ( 'NONE', #129072, #65285, #106580 ) ;
#130400=EDGE_CURVE ( 'NONE', #89147, #771, #86536, .T. ) ;
#130402=EDGE_CURVE ( 'NONE', #80109, #51668, #178, .T. ) ;
#130404=ORIENTED_EDGE ( 'NONE', *, *, #135461, .F. ) ;
#130407=EDGE_LOOP ( 'NONE', ( #95627, #80501, #1351, #72790 ) ) ;
#130408=ADVANCED_FACE ( 'NONE', ( #32135 ), #90827, .T. ) ;
#130409=FACE_OUTER_BOUND ( 'NONE', #136819, .T. ) ;
#130410=VECTOR ( 'NONE', #87230, 1000.000000000000227 ) ;
#130411=FACE_OUTER_BOUND ( 'NONE', #54961, .T. ) ;
#130412=EDGE_LOOP ( 'NONE', ( #7260, #19537, #92083, #47689 ) ) ;
#130413=CARTESIAN_POINT ( 'NONE',  ( -19.49999999999986144, -10.53360074219763121, 5.000000000000000000 ) ) ;
#130414=LINE ( 'NONE', #31802, #25714 ) ;
#130415=EDGE_CURVE ( 'NONE', #74972, #84117, #133608, .T. ) ;
#130417=ORIENTED_EDGE ( 'NONE', *, *, #75456, .T. ) ;
#130418=PLANE ( 'NONE',  #253 ) ;
#130419=DIRECTION ( 'NONE',  ( -0.3543493200069162685, -0.000000000000000000, -0.9351131265310288487 ) ) ;
#130423=VERTEX_POINT ( 'NONE', #135060 ) ;
#130424=VERTEX_POINT ( 'NONE', #102422 ) ;
#130425=ORIENTED_EDGE ( 'NONE', *, *, #30027, .T. ) ;
#130426=DIRECTION ( 'NONE',  ( 1.000000000000000000, 0.000000000000000000, 0.000000000000000000 ) ) ;
#130429=VECTOR ( 'NONE', #101139, 999.9999999999998863 ) ;
#130430=ADVANCED_FACE ( 'NONE', ( #79972 ), #92209, .F. ) ;
#130431=CARTESIAN_POINT ( 'NONE',  ( 14.70025512860841133, -27.71228299555195917, 4.000000000000000000 ) ) ;
#130432=CARTESIAN_POINT ( 'NONE',  ( 34.49999999999975842, 12.05432934483081908, 4.994342998332162331 ) ) ;
#130435=VERTEX_POINT ( 'NONE', #113982 ) ;
#130436=CARTESIAN_POINT ( 'NONE',  ( 24.48921356237309510, -27.52281430457072631, 5.000000000000000000 ) ) ;
#130438=EDGE_LOOP ( 'NONE', ( #15012, #58094, #57293, #119370 ) ) ;
#130439=EDGE_CURVE ( 'NONE', #39023, #86810, #58955, .T. ) ;
#130440=AXIS2_PLACEMENT_3D ( 'NONE', #94815, #117984, #115848 ) ;
#130441=VECTOR ( 'NONE', #40612, 999.9999999999998863 ) ;
#130444=CARTESIAN_POINT ( 'NONE',  ( -11.01844734635663769, 18.75929247661552424, 20.33588619593445301 ) ) ;
#130446=CARTESIAN_POINT ( 'NONE',  ( 25.49999999999982947, -4.533600742197692490, 5.000000000000000000 ) ) ;
#130447=CARTESIAN_POINT ( 'NONE',  ( 18.79289321881333308, -14.24070752338413826, 5.000000000000000000 ) ) ;
#130448=EDGE_CURVE ( 'NONE', #99882, #2363, #79263, .T. ) ;
#130449=CARTESIAN_POINT ( 'NONE',  ( -13.49999999999991118, -7.420205493532915142, -2.617629953481283245 ) ) ;
#130450=AXIS2_PLACEMENT_3D ( 'NONE', #37152, #5911, #61107 ) ;
#130452=DIRECTION ( 'NONE',  ( -0.7071067811865486830, 0.7071067811865464625, 0.000000000000000000 ) ) ;
#130453=CARTESIAN_POINT ( 'NONE',  ( 1.748455871324237965, -11.24070752338417201, 10.39518518046008744 ) ) ;
#130455=EDGE_CURVE ( 'NONE', #89594, #116711, #24828, .T. ) ;
#130456=EDGE_LOOP ( 'NONE', ( #95785, #119875, #53686, #86266, #10774 ) ) ;
#130457=DIRECTION ( 'NONE',  ( -0.7071067811865487940, 0.7071067811865463515, -0.000000000000000000 ) ) ;
#130458=CARTESIAN_POINT ( 'NONE',  ( -13.49999999999990052, 13.56627193232213813, -10.57019076586071904 ) ) ;
#130459=ORIENTED_EDGE ( 'NONE', *, *, #11276, .F. ) ;
#130460=DIRECTION ( 'NONE',  ( -0.7071067811865487940, 0.7071067811865463515, 0.000000000000000000 ) ) ;
#130461=VERTEX_POINT ( 'NONE', #124855 ) ;
#130465=VECTOR ( 'NONE', #91245, 1000.000000000000000 ) ;
#130466=EDGE_CURVE ( 'NONE', #38343, #1788, #34283, .T. ) ;
#130472=CARTESIAN_POINT ( 'NONE',  ( 2.111623618947573888, 9.759292476615621936, 17.35367589129212362 ) ) ;
#130473=ADVANCED_FACE ( 'NONE', ( #45195 ), #101667, .F. ) ;
#130474=CARTESIAN_POINT ( 'NONE',  ( 54.48921356237310221, -27.52281430457093236, 5.000000000000000000 ) ) ;
#130475=DIRECTION ( 'NONE',  ( -0.7071067811865486830, 0.7071067811865464625, 0.000000000000000000 ) ) ;
#130476=CARTESIAN_POINT ( 'NONE',  ( -17.21837311707493257, 21.74787736706806385, 4.999607392498047531 ) ) ;
#130477=VECTOR ( 'NONE', #119917, 1000.000000000000000 ) ;
#130478=CARTESIAN_POINT ( 'NONE',  ( 17.99999999999987566, -3.412538124160721331, 4.000000000000000000 ) ) ;
#130479=LINE ( 'NONE', #41294, #32082 ) ;
#130480=FACE_OUTER_BOUND ( 'NONE', #120236, .T. ) ;
#130481=VECTOR ( 'NONE', #143137, 999.9999999999998863 ) ;
#130483=ORIENTED_EDGE ( 'NONE', *, *, #25078, .T. ) ;
#130485=ORIENTED_EDGE ( 'NONE', *, *, #46505, .F. ) ;
#130488=ORIENTED_EDGE ( 'NONE', *, *, #96906, .F. ) ;
#130489=( BOUNDED_CURVE ( )  B_SPLINE_CURVE ( 3, ( #58528, #59911, #47635, #91796 ),
 .UNSPECIFIED., .F., .T. ) 
 B_SPLINE_CURVE_WITH_KNOTS ( ( 4, 4 ),
 ( 5.043186909253404515, 5.074607125596347856 ),
 .UNSPECIFIED. ) 
 CURVE ( )  GEOMETRIC_REPRESENTATION_ITEM ( )  RATIONAL_B_SPLINE_CURVE ( ( 1.000000000000000000, 0.9999177325257868620, 0.9999177325257868620, 1.000000000000000000 ) ) 
 REPRESENTATION_ITEM ( '' )  );
#130490=VECTOR ( 'NONE', #71784, 1000.000000000000227 ) ;
#130491=EDGE_LOOP ( 'NONE', ( #851, #27863, #26164, #85437 ) ) ;
#130492=DIRECTION ( 'NONE',  ( -0.7071067811865486830, -0.7071067811865464625, 0.000000000000000000 ) ) ;
#130493=DIRECTION ( 'NONE',  ( 0.7071067811865487940, 0.7071067811865463515, -0.000000000000000000 ) ) ;
#130494=EDGE_CURVE ( 'NONE', #10056, #23517, #22648, .T. ) ;
#130495=CARTESIAN_POINT ( 'NONE',  ( -44.99451991528749772, 28.92564299267969474, 4.000000000000000000 ) ) ;
#130496=ORIENTED_EDGE ( 'NONE', *, *, #33259, .T. ) ;
#130498=ORIENTED_EDGE ( 'NONE', *, *, #61549, .T. ) ;
#130499=LINE ( 'NONE', #19567, #113979 ) ;
#130500=VECTOR ( 'NONE', #83021, 1000.000000000000227 ) ;
#130501=ADVANCED_FACE ( 'NONE', ( #67661 ), #90070, .F. ) ;
#130502=LINE ( 'NONE', #74700, #61302 ) ;
#130503=AXIS2_PLACEMENT_3D ( 'NONE', #133339, #78974, #89806 ) ;
#130508=CARTESIAN_POINT ( 'NONE',  ( 26.99451991528749417, 28.92564299267956685, 4.000000000000000000 ) ) ;
#130509=LINE ( 'NONE', #32621, #109100 ) ;
#130510=ORIENTED_EDGE ( 'NONE', *, *, #115391, .F. ) ;
#130511=ORIENTED_EDGE ( 'NONE', *, *, #102636, .T. ) ;
#130513=ORIENTED_EDGE ( 'NONE', *, *, #118601, .F. ) ;
#130514=CARTESIAN_POINT ( 'NONE',  ( -27.70710678118634007, 2.259292476615696099, 5.000000000000000000 ) ) ;
#130515=VECTOR ( 'NONE', #99887, 999.9999999999998863 ) ;
#130516=DIRECTION ( 'NONE',  ( 0.7071067811865487940, 0.7071067811865463515, -0.000000000000000000 ) ) ;
#130517=DIRECTION ( 'NONE',  ( 0.3543493200069162685, -0.000000000000000000, -0.9351131265310288487 ) ) ;
#130519=ORIENTED_EDGE ( 'NONE', *, *, #102074, .F. ) ;
#130520=PLANE ( 'NONE',  #117779 ) ;
#130522=CARTESIAN_POINT ( 'NONE',  ( 0.8365287112654871127, 15.75929247661555443, 9.299976744542924223 ) ) ;
#130523=DIRECTION ( 'NONE',  ( -0.7071067811865486830, 0.7071067811865464625, 0.000000000000000000 ) ) ;
#130526=LINE ( 'NONE', #143515, #72523 ) ;
#130530=ORIENTED_EDGE ( 'NONE', *, *, #132635, .F. ) ;
#130531=ADVANCED_FACE ( 'NONE', ( #48037 ), #36429, .T. ) ;
#130532=AXIS2_PLACEMENT_3D ( 'NONE', #107899, #18028, #61612 ) ;
#130533=PLANE ( 'NONE',  #7622 ) ;
#130534=DIRECTION ( 'NONE',  ( -0.000000000000000000, 0.3543493200069153248, 0.9351131265310292928 ) ) ;
#130535=ORIENTED_EDGE ( 'NONE', *, *, #142821, .F. ) ;
#130536=DIRECTION ( 'NONE',  ( 1.000000000000000000, 0.000000000000000000, 0.000000000000000000 ) ) ;
#130539=CARTESIAN_POINT ( 'NONE',  ( 36.48921356237310221, -27.52281430457080802, 5.000000000000000000 ) ) ;
#130540=CARTESIAN_POINT ( 'NONE',  ( -5.816011393731002066, 28.73617430169783304, 5.000000000000000000 ) ) ;
#130542=CARTESIAN_POINT ( 'NONE',  ( -15.18398860626900237, 28.73617430169797871, 5.000000000000000000 ) ) ;
#130545=DIRECTION ( 'NONE',  ( -0.000000000000000000, -0.3543493200069152693, 0.9351131265310292928 ) ) ;
#130546=CARTESIAN_POINT ( 'NONE',  ( -42.48921356237308800, -27.52281430457085065, 5.000000000000000000 ) ) ;
#130547=PLANE ( 'NONE',  #74304 ) ;
#130548=VERTEX_POINT ( 'NONE', #3071 ) ;
#130549=AXIS2_PLACEMENT_3D ( 'NONE', #4855, #136845, #81794 ) ;
#130550=VERTEX_POINT ( 'NONE', #2325 ) ;
#130551=ORIENTED_EDGE ( 'NONE', *, *, #134834, .T. ) ;
#130553=ORIENTED_EDGE ( 'NONE', *, *, #96005, .T. ) ;
#130554=EDGE_CURVE ( 'NONE', #24092, #120463, #912, .T. ) ;
#130555=VERTEX_POINT ( 'NONE', #68376 ) ;
#130556=VERTEX_POINT ( 'NONE', #112554 ) ;
#130557=DIRECTION ( 'NONE',  ( 1.000000000000000000, 0.000000000000000000, 0.000000000000000000 ) ) ;
#130558=CARTESIAN_POINT ( 'NONE',  ( 0.000000000000000000, 0.000000000000000000, 5.000000000000000000 ) ) ;
#130562=DIRECTION ( 'NONE',  ( -0.6830127018922180770, -0.6830127018922204085, -0.2588190451025213501 ) ) ;
#130564=LINE ( 'NONE', #31249, #69704 ) ;
#130566=ORIENTED_EDGE ( 'NONE', *, *, #32912, .T. ) ;
#130567=EDGE_CURVE ( 'NONE', #2768, #113494, #72675, .T. ) ;
#130568=EDGE_CURVE ( 'NONE', #94977, #45414, #106644, .T. ) ;
#130571=VECTOR ( 'NONE', #6130, 999.9999999999998863 ) ;
#130572=DIRECTION ( 'NONE',  ( -0.3543493200069162685, -0.000000000000000000, -0.9351131265310288487 ) ) ;
#130573=CARTESIAN_POINT ( 'NONE',  ( 0.000000000000000000, 0.000000000000000000, 5.000000000000000000 ) ) ;
#130574=FACE_OUTER_BOUND ( 'NONE', #97495, .T. ) ;
#130576=DIRECTION ( 'NONE',  ( 1.000000000000000000, 0.000000000000000000, 0.000000000000000000 ) ) ;
#130577=EDGE_CURVE ( 'NONE', #54392, #77801, #50167, .T. ) ;
#130578=ADVANCED_FACE ( 'NONE', ( #49481 ), #18196, .F. ) ;
#130579=VECTOR ( 'NONE', #6744, 1000.000000000000227 ) ;
#130580=VERTEX_POINT ( 'NONE', #5895 ) ;
#130581=EDGE_LOOP ( 'NONE', ( #56179, #64392, #37677, #32545 ) ) ;
#130583=EDGE_CURVE ( 'NONE', #143522, #131909, #88547, .T. ) ;
#130584=ORIENTED_EDGE ( 'NONE', *, *, #71464, .T. ) ;
#130586=ADVANCED_FACE ( 'NONE', ( #62469 ), #140039, .F. ) ;
#130589=CARTESIAN_POINT ( 'NONE',  ( 14.99999999999989164, -22.06887692260759692, 4.000000000000000000 ) ) ;
#130590=AXIS2_PLACEMENT_3D ( 'NONE', #134242, #112480, #34935 ) ;
#130591=PLANE ( 'NONE',  #130252 ) ;
#130593=LINE ( 'NONE', #21808, #16372 ) ;
#130594=EDGE_CURVE ( 'NONE', #83105, #89365, #137177, .T. ) ;
#130596=VECTOR ( 'NONE', #106566, 1000.000000000000000 ) ;
#130599=CARTESIAN_POINT ( 'NONE',  ( -24.18398860626899705, 28.73617430169804265, 5.000000000000000000 ) ) ;
#130600=VERTEX_POINT ( 'NONE', #139339 ) ;
#130601=CARTESIAN_POINT ( 'NONE',  ( 0.000000000000000000, 0.000000000000000000, 5.000000000000000000 ) ) ;
#130602=CARTESIAN_POINT ( 'NONE',  ( -17.99999999999987566, -2.904428200921318481, -6.989807076074900039 ) ) ;
#130603=CARTESIAN_POINT ( 'NONE',  ( 11.51078643762690490, -27.52281430457047406, 5.000000000000000000 ) ) ;
#130604=AXIS2_PLACEMENT_3D ( 'NONE', #59743, #72065, #117628 ) ;
#130605=EDGE_CURVE ( 'NONE', #80902, #141246, #27672, .T. ) ;
#130606=CARTESIAN_POINT ( 'NONE',  ( 39.29974487139159578, -27.71228299555233576, 4.000000000000000000 ) ) ;
#130607=ORIENTED_EDGE ( 'NONE', *, *, #115866, .T. ) ;
#130609=VECTOR ( 'NONE', #62562, 1000.000000000000000 ) ;
#130610=VERTEX_POINT ( 'NONE', #81390 ) ;
#130611=CARTESIAN_POINT ( 'NONE',  ( 8.510786437626906675, -27.52281430457049183, 5.000000000000000000 ) ) ;
#130612=CARTESIAN_POINT ( 'NONE',  ( -30.18398860626900060, 28.73617430169808173, 5.000000000000000000 ) ) ;
#130613=LINE ( 'NONE', #18967, #54842 ) ;
#130615=EDGE_CURVE ( 'NONE', #132730, #24067, #114678, .T. ) ;
#130616=VECTOR ( 'NONE', #101738, 1000.000000000000227 ) ;
#130617=VECTOR ( 'NONE', #103191, 999.9999999999998863 ) ;
#130620=VERTEX_POINT ( 'NONE', #59634 ) ;
#130621=CARTESIAN_POINT ( 'NONE',  ( -25.36246187583883582, 22.22500000000000853, 4.000000000000000000 ) ) ;
#130622=ORIENTED_EDGE ( 'NONE', *, *, #115857, .F. ) ;
#130623=EDGE_LOOP ( 'NONE', ( #57422, #133465, #94599, #8600 ) ) ;
#130624=VECTOR ( 'NONE', #37468, 999.9999999999998863 ) ;
#130625=VERTEX_POINT ( 'NONE', #17511 ) ;
#130627=FACE_OUTER_BOUND ( 'NONE', #59653, .T. ) ;
#130628=CARTESIAN_POINT ( 'NONE',  ( -25.49999999999982236, 7.466399257802184053, 5.000000000000000000 ) ) ;
#130629=ORIENTED_EDGE ( 'NONE', *, *, #56423, .T. ) ;
#130630=CARTESIAN_POINT ( 'NONE',  ( -27.18398860626900060, 28.73617430169806042, 5.000000000000000000 ) ) ;
#130631=ADVANCED_FACE ( 'NONE', ( #103789 ), #104526, .F. ) ;
#130632=FACE_OUTER_BOUND ( 'NONE', #450, .T. ) ;
#130636=DIRECTION ( 'NONE',  ( 1.000000000000000000, 0.000000000000000000, 0.000000000000000000 ) ) ;
#130637=FACE_BOUND ( 'NONE', #25760, .T. ) ;
#130638=VERTEX_POINT ( 'NONE', #63899 ) ;
#130640=DIRECTION ( 'NONE',  ( -0.3543493200069163240, 0.000000000000000000, 0.9351131265310288487 ) ) ;
#130641=EDGE_LOOP ( 'NONE', ( #61763, #89641, #30036, #131803 ) ) ;
#130643=VERTEX_POINT ( 'NONE', #96471 ) ;
#130644=ORIENTED_EDGE ( 'NONE', *, *, #83954, .T. ) ;
#130645=CARTESIAN_POINT ( 'NONE',  ( -17.67183060077635304, 14.25929247661557753, 4.000000000000000000 ) ) ;
#130646=EDGE_CURVE ( 'NONE', #73032, #129071, #140714, .T. ) ;
#130647=ORIENTED_EDGE ( 'NONE', *, *, #53, .F. ) ;
#130649=ORIENTED_EDGE ( 'NONE', *, *, #72208, .T. ) ;
#130650=CARTESIAN_POINT ( 'NONE',  ( -31.49999999999978684, -4.216083040037277740, -7.486842126848585188 ) ) ;
#130651=CARTESIAN_POINT ( 'NONE',  ( -11.99999999999991296, 16.93112307739200872, 4.000000000000000000 ) ) ;
#130652=EDGE_CURVE ( 'NONE', #105689, #81537, #31969, .T. ) ;
#130654=DIRECTION ( 'NONE',  ( 0.7071067811865487940, 0.7071067811865463515, -0.000000000000000000 ) ) ;
#130655=FACE_OUTER_BOUND ( 'NONE', #7416, .T. ) ;
#130656=DIRECTION ( 'NONE',  ( 0.7071067811865487940, -0.7071067811865463515, 0.000000000000000000 ) ) ;
#130657=CARTESIAN_POINT ( 'NONE',  ( -48.48921356237309510, -27.52281430457089328, 5.000000000000000000 ) ) ;
#130658=LINE ( 'NONE', #21864, #13399 ) ;
#130659=FACE_OUTER_BOUND ( 'NONE', #105980, .T. ) ;
#130660=DIRECTION ( 'NONE',  ( -1.000000000000000000, 0.000000000000000000, 0.000000000000000000 ) ) ;
#130661=ORIENTED_EDGE ( 'NONE', *, *, #128065, .T. ) ;
#130662=VERTEX_POINT ( 'NONE', #42873 ) ;
#130665=PLANE ( 'NONE',  #44363 ) ;
#130666=ORIENTED_EDGE ( 'NONE', *, *, #113853, .F. ) ;
#130667=ORIENTED_EDGE ( 'NONE', *, *, #6976, .T. ) ;
#130668=ORIENTED_EDGE ( 'NONE', *, *, #119827, .T. ) ;
#130669=DIRECTION ( 'NONE',  ( -0.7071067811865487940, 0.7071067811865463515, -0.000000000000000000 ) ) ;
#130671=ADVANCED_FACE ( 'NONE', ( #54465 ), #130591, .F. ) ;
#130672=ADVANCED_FACE ( 'NONE', ( #87779 ), #119655, .F. ) ;
#130673=DIRECTION ( 'NONE',  ( 0.6830127018922180770, -0.6830127018922204085, -0.2588190451025213501 ) ) ;
#130674=ORIENTED_EDGE ( 'NONE', *, *, #36217, .F. ) ;
#130675=DIRECTION ( 'NONE',  ( 1.000000000000000000, 0.000000000000000000, 0.000000000000000000 ) ) ;
#130676=VECTOR ( 'NONE', #32780, 1000.000000000000000 ) ;
#130677=CARTESIAN_POINT ( 'NONE',  ( -21.48921356237309155, -27.52281430457070499, 5.000000000000000000 ) ) ;
#130678=AXIS2_PLACEMENT_3D ( 'NONE', #109510, #110203, #72642 ) ;
#130680=DIRECTION ( 'NONE',  ( 0.7071067811865487940, -0.7071067811865463515, 0.000000000000000000 ) ) ;
#130681=VERTEX_POINT ( 'NONE', #129853 ) ;
#130683=ADVANCED_FACE ( 'NONE', ( #29812 ), #108063, .F. ) ;
#130684=VECTOR ( 'NONE', #77264, 1000.000000000000227 ) ;
#130685=CARTESIAN_POINT ( 'NONE',  ( -36.48921356237310221, -27.52281430457080802, 5.000000000000000000 ) ) ;
#130686=CARTESIAN_POINT ( 'NONE',  ( -30.49816348513938280, -17.24070752338409918, 8.407044977365297100 ) ) ;
#130687=CARTESIAN_POINT ( 'NONE',  ( 9.516654386410381861, 22.22500000000000142, 4.500000000000000888 ) ) ;
#130688=ORIENTED_EDGE ( 'NONE', *, *, #78074, .T. ) ;
#130691=CARTESIAN_POINT ( 'NONE',  ( 10.49999999999991829, 16.18958161055403622, -11.56426086740808934 ) ) ;
#130693=EDGE_CURVE ( 'NONE', #83571, #115863, #63209, .T. ) ;
#130694=PLANE ( 'NONE',  #3166 ) ;
#130695=EDGE_LOOP ( 'NONE', ( #44720, #72840, #16868 ) ) ;
#130696=EDGE_CURVE ( 'NONE', #111034, #37058, #86366, .T. ) ;
#130699=VECTOR ( 'NONE', #62476, 1000.000000000000000 ) ;
#130700=DIRECTION ( 'NONE',  ( -0.6830127018922180770, -0.6830127018922204085, -0.2588190451025213501 ) ) ;
#130702=ORIENTED_EDGE ( 'NONE', *, *, #125536, .F. ) ;
#130704=CARTESIAN_POINT ( 'NONE',  ( 34.92499999999998295, 22.22500000000000142, 4.500000000000000888 ) ) ;
#130705=EDGE_LOOP ( 'NONE', ( #128601, #120986, #76988, #44237 ) ) ;
#130707=PLANE ( 'NONE',  #69269 ) ;
#130708=AXIS2_PLACEMENT_3D ( 'NONE', #101962, #1191, #112140 ) ;
#130709=EDGE_LOOP ( 'NONE', ( #89338, #82869, #83732, #77660 ) ) ;
#130710=EDGE_CURVE ( 'NONE', #40283, #18415, #87067, .T. ) ;
#130711=EDGE_LOOP ( 'NONE', ( #43678, #100818, #30872, #44784 ) ) ;
#130713=CARTESIAN_POINT ( 'NONE',  ( 7.771493228613311821, 20.25929247661551358, 7.808871592221786173 ) ) ;
#130714=AXIS2_PLACEMENT_3D ( 'NONE', #87494, #8451, #43995 ) ;
#130720=ORIENTED_EDGE ( 'NONE', *, *, #104835, .F. ) ;
#130722=CARTESIAN_POINT ( 'NONE',  ( -14.99999999999989697, 16.93112307739200872, 4.000000000000000000 ) ) ;
#130723=DIRECTION ( 'NONE',  ( -0.7071067811865486830, 0.7071067811865464625, 0.000000000000000000 ) ) ;
#130726=CARTESIAN_POINT ( 'NONE',  ( -21.77004279457778324, 21.73644205237997795, 5.000000000000000888 ) ) ;
#130727=VECTOR ( 'NONE', #71440, 999.9999999999998863 ) ;
#130728=ORIENTED_EDGE ( 'NONE', *, *, #94677, .T. ) ;
#130729=ORIENTED_EDGE ( 'NONE', *, *, #56373, .T. ) ;
#130730=DIRECTION ( 'NONE',  ( 1.000000000000000000, 0.000000000000000000, 0.000000000000000000 ) ) ;
#130731=EDGE_LOOP ( 'NONE', ( #98526, #29081, #94002, #70069 ) ) ;
#130732=EDGE_LOOP ( 'NONE', ( #78518, #110796, #7510 ) ) ;
#130733=FACE_OUTER_BOUND ( 'NONE', #9520, .T. ) ;
#130734=DIRECTION ( 'NONE',  ( 1.000000000000000000, 0.000000000000000000, 0.000000000000000000 ) ) ;
#130735=EDGE_LOOP ( 'NONE', ( #27713, #141165, #131180 ) ) ;
#130736=CARTESIAN_POINT ( 'NONE',  ( -60.48921356237309510, -27.52281430457097500, 5.000000000000000000 ) ) ;
#130737=DIRECTION ( 'NONE',  ( -0.000000000000000000, -0.3543493200069152693, 0.9351131265310292928 ) ) ;
#130738=LINE ( 'NONE', #40850, #97243 ) ;
#130739=DIRECTION ( 'NONE',  ( 0.6830127018922181881, 0.6830127018922202975, -0.2588190451025214056 ) ) ;
#130740=CARTESIAN_POINT ( 'NONE',  ( 50.99451991528749062, 28.92564299267973738, 4.000000000000000000 ) ) ;
#130741=EDGE_LOOP ( 'NONE', ( #36210, #23193, #13528, #127831 ) ) ;
#130742=DIRECTION ( 'NONE',  ( -0.7071067811865486830, -0.7071067811865464625, 0.000000000000000000 ) ) ;
#130743=DIRECTION ( 'NONE',  ( -0.7071067811865487940, 0.7071067811865463515, 0.000000000000000000 ) ) ;
#130744=CARTESIAN_POINT ( 'NONE',  ( -7.171830600776419651, 9.759292476615614831, 4.000000000000000000 ) ) ;
#130746=LINE ( 'NONE', #6747, #72867 ) ;
#130748=DIRECTION ( 'NONE',  ( -0.000000000000000000, 0.3543493200069153248, 0.9351131265310292928 ) ) ;
#130750=EDGE_CURVE ( 'NONE', #22993, #30236, #76196, .T. ) ;
#130751=DIRECTION ( 'NONE',  ( 0.3543493200069162685, -0.000000000000000000, -0.9351131265310288487 ) ) ;
#130752=ORIENTED_EDGE ( 'NONE', *, *, #39546, .F. ) ;
#130757=EDGE_CURVE ( 'NONE', #48106, #132436, #118968, .T. ) ;
#130758=DIRECTION ( 'NONE',  ( 0.000000000000000000, 0.000000000000000000, 1.000000000000000000 ) ) ;
#130759=ADVANCED_FACE ( 'NONE', ( #97943 ), #127448, .F. ) ;
#130760=DIRECTION ( 'NONE',  ( -0.7071067811865486830, -0.7071067811865464625, 0.000000000000000000 ) ) ;
#130761=ORIENTED_EDGE ( 'NONE', *, *, #25009, .T. ) ;
#130762=EDGE_CURVE ( 'NONE', #102338, #16517, #137637, .T. ) ;
#130763=LINE ( 'NONE', #136788, #17746 ) ;
#130765=CARTESIAN_POINT ( 'NONE',  ( 13.20450575203696886, 4.382956123802139281, 4.000000000000000000 ) ) ;
#130767=ORIENTED_EDGE ( 'NONE', *, *, #16654, .T. ) ;
#130768=EDGE_CURVE ( 'NONE', #15864, #62440, #52044, .T. ) ;
#130770=ORIENTED_EDGE ( 'NONE', *, *, #124018, .F. ) ;
#130771=ORIENTED_EDGE ( 'NONE', *, *, #138003, .T. ) ;
#130772=FACE_OUTER_BOUND ( 'NONE', #105341, .T. ) ;
#130773=LINE ( 'NONE', #54627, #114815 ) ;
#130774=LINE ( 'NONE', #84412, #351 ) ;
#130775=EDGE_CURVE ( 'NONE', #56766, #26207, #115110, .T. ) ;
#130776=LINE ( 'NONE', #52457, #30 ) ;
#130777=ORIENTED_EDGE ( 'NONE', *, *, #60540, .F. ) ;
#130778=CARTESIAN_POINT ( 'NONE',  ( -23.28769006033954980, -21.73547319004781286, 4.999917730833664642 ) ) ;
#130779=EDGE_CURVE ( 'NONE', #8157, #64105, #26302, .T. ) ;
#130780=LINE ( 'NONE', #31444, #51223 ) ;
#130781=CARTESIAN_POINT ( 'NONE',  ( -19.17183060077634238, -11.24070752338416490, 4.000000000000000000 ) ) ;
#130782=EDGE_LOOP ( 'NONE', ( #89455, #2665, #1867, #61928 ) ) ;
#130784=LINE ( 'NONE', #9669, #106329 ) ;
#130786=DIRECTION ( 'NONE',  ( 1.000000000000000000, -0.000000000000000000, 0.000000000000000000 ) ) ;
#130787=CARTESIAN_POINT ( 'NONE',  ( 30.32816939922332367, -21.74070752338405654, 4.000000000000000000 ) ) ;
#130788=CARTESIAN_POINT ( 'NONE',  ( -2.671830600776449405, -3.740707523384251942, 4.000000000000000000 ) ) ;
#130790=VECTOR ( 'NONE', #34642, 1000.000000000000000 ) ;
#130791=ORIENTED_EDGE ( 'NONE', *, *, #17404, .F. ) ;
#130792=PLANE ( 'NONE',  #77791 ) ;
#130794=AXIS2_PLACEMENT_3D ( 'NONE', #64755, #132897, #893 ) ;
#130795=DIRECTION ( 'NONE',  ( -0.6830127018922181881, 0.6830127018922202975, -0.2588190451025214056 ) ) ;
#130796=LINE ( 'NONE', #20550, #124166 ) ;
#130797=EDGE_LOOP ( 'NONE', ( #97695, #69638, #60876, #115439 ) ) ;
#130798=VERTEX_POINT ( 'NONE', #29551 ) ;
#130799=EDGE_CURVE ( 'NONE', #103522, #137089, #39760, .T. ) ;
#130800=CARTESIAN_POINT ( 'NONE',  ( 20.99999999999983658, -13.39766691384881803, -10.96608748226470986 ) ) ;
#130801=VERTEX_POINT ( 'NONE', #60077 ) ;
#130802=EDGE_LOOP ( 'NONE', ( #55914, #3725, #139060, #104585 ) ) ;
#130804=CARTESIAN_POINT ( 'NONE',  ( -5.510786437626906675, -27.52281430457051314, 5.000000000000000000 ) ) ;
#130805=ORIENTED_EDGE ( 'NONE', *, *, #55010, .T. ) ;
#130806=DIRECTION ( 'NONE',  ( -0.6830127018922180770, -0.6830127018922204085, -0.2588190451025213501 ) ) ;
#130807=DIRECTION ( 'NONE',  ( 0.7071067811865487940, 0.7071067811865463515, -0.000000000000000000 ) ) ;
#130808=EDGE_CURVE ( 'NONE', #132249, #139004, #117259, .T. ) ;
#130809=CARTESIAN_POINT ( 'NONE',  ( -0.5116860592843074373, 6.759292476615660128, 16.35960578974469826 ) ) ;
#130810=FACE_BOUND ( 'NONE', #88645, .T. ) ;
#130811=DIRECTION ( 'NONE',  ( -0.7071067811865486830, 0.7071067811865464625, 0.000000000000000000 ) ) ;
#130813=FACE_OUTER_BOUND ( 'NONE', #4271, .T. ) ;
#130814=LINE ( 'NONE', #110434, #24990 ) ;
#130816=PLANE ( 'NONE',  #83422 ) ;
#130818=VECTOR ( 'NONE', #98625, 1000.000000000000000 ) ;
#130819=ORIENTED_EDGE ( 'NONE', *, *, #118328, .F. ) ;
#130820=AXIS2_PLACEMENT_3D ( 'NONE', #83046, #127246, #81646 ) ;
#130822=ORIENTED_EDGE ( 'NONE', *, *, #29621, .F. ) ;
#130824=ORIENTED_EDGE ( 'NONE', *, *, #94255, .F. ) ;
#130825=VECTOR ( 'NONE', #77503, 999.9999999999998863 ) ;
#130826=LINE ( 'NONE', #143098, #88362 ) ;
#130827=EDGE_CURVE ( 'NONE', #47269, #49530, #61524, .T. ) ;
#130828=EDGE_LOOP ( 'NONE', ( #134196, #6959, #21138, #90077 ) ) ;
#130831=DIRECTION ( 'NONE',  ( -0.000000000000000000, 0.3543493200069153248, 0.9351131265310292928 ) ) ;
#130835=CARTESIAN_POINT ( 'NONE',  ( 10.49999999999993250, -5.568876922607757685, 4.000000000000000000 ) ) ;
#130836=PLANE ( 'NONE',  #14528 ) ;
#130837=DIRECTION ( 'NONE',  ( -0.3543493200069162685, -0.000000000000000000, -0.9351131265310288487 ) ) ;
#130838=VERTEX_POINT ( 'NONE', #83988 ) ;
#130839=PLANE ( 'NONE',  #74718 ) ;
#130840=ORIENTED_EDGE ( 'NONE', *, *, #9171, .F. ) ;
#130843=VERTEX_POINT ( 'NONE', #104246 ) ;
#130844=ORIENTED_EDGE ( 'NONE', *, *, #2628, .F. ) ;
#130845=EDGE_CURVE ( 'NONE', #52797, #70280, #41153, .T. ) ;
#130846=ORIENTED_EDGE ( 'NONE', *, *, #99306, .T. ) ;
#130847=EDGE_CURVE ( 'NONE', #115630, #35253, #91093, .T. ) ;
#130854=ORIENTED_EDGE ( 'NONE', *, *, #34176, .T. ) ;
#130856=VERTEX_POINT ( 'NONE', #28865 ) ;
#130858=DIRECTION ( 'NONE',  ( -0.7071067811865486830, -0.7071067811865464625, -0.000000000000000000 ) ) ;
#130859=CARTESIAN_POINT ( 'NONE',  ( -26.99451991528749417, 28.92564299267956685, 4.000000000000000000 ) ) ;
#130860=ORIENTED_EDGE ( 'NONE', *, *, #93534, .T. ) ;
#130861=VERTEX_POINT ( 'NONE', #49209 ) ;
#130862=CARTESIAN_POINT ( 'NONE',  ( 35.99451991528749772, 28.92564299267963079, 4.000000000000000000 ) ) ;
#130863=CARTESIAN_POINT ( 'NONE',  ( 15.18398860626900237, 28.73617430169797871, 5.000000000000000000 ) ) ;
#130864=DIRECTION ( 'NONE',  ( 1.000000000000000000, 0.000000000000000000, 0.000000000000000000 ) ) ;
#130865=ORIENTED_EDGE ( 'NONE', *, *, #65, .T. ) ;
#130867=EDGE_LOOP ( 'NONE', ( #50958, #93634, #7560, #13884 ) ) ;
#130868=ADVANCED_FACE ( 'NONE', ( #51336 ), #95524, .F. ) ;
#130870=ORIENTED_EDGE ( 'NONE', *, *, #10782, .T. ) ;
#130871=CARTESIAN_POINT ( 'NONE',  ( 30.18398860626900060, 28.73617430169808173, 5.000000000000000000 ) ) ;
#130872=LINE ( 'NONE', #96743, #29976 ) ;
#130873=CARTESIAN_POINT ( 'NONE',  ( 34.49999999999975842, -8.945670655168960650, 4.994342998332163219 ) ) ;
#130874=LINE ( 'NONE', #62755, #19074 ) ;
#130876=EDGE_CURVE ( 'NONE', #24466, #125243, #38315, .T. ) ;
#130878=EDGE_LOOP ( 'NONE', ( #1903, #13429, #72550, #66075 ) ) ;
#130879=EDGE_CURVE ( 'NONE', #4040, #30662, #115825, .T. ) ;
#130880=CARTESIAN_POINT ( 'NONE',  ( -30.18398860626900060, 28.73617430169808173, 5.000000000000000000 ) ) ;
#130881=ORIENTED_EDGE ( 'NONE', *, *, #56479, .T. ) ;
#130882=CARTESIAN_POINT ( 'NONE',  ( -41.99451991528749062, 28.92564299267967343, 4.000000000000000000 ) ) ;
#130885=DIRECTION ( 'NONE',  ( 1.000000000000000000, 0.000000000000000000, 0.000000000000000000 ) ) ;
#130886=FACE_OUTER_BOUND ( 'NONE', #113706, .T. ) ;
#130888=VECTOR ( 'NONE', #142678, 1000.000000000000000 ) ;
#130889=VERTEX_POINT ( 'NONE', #83242 ) ;
#130890=DIRECTION ( 'NONE',  ( -0.7071067811865487940, 0.7071067811865463515, -0.000000000000000000 ) ) ;
#130891=LINE ( 'NONE', #117808, #122893 ) ;
#130892=LINE ( 'NONE', #142472, #111731 ) ;
#130894=CARTESIAN_POINT ( 'NONE',  ( -7.499999999999951150, -12.08601207473289740, -10.46905243149092612 ) ) ;
#130897=( BOUNDED_CURVE ( )  B_SPLINE_CURVE ( 3, ( #119850, #19146, #127930, #75681 ),
 .UNSPECIFIED., .F., .F. ) 
 B_SPLINE_CURVE_WITH_KNOTS ( ( 4, 4 ),
 ( 5.106027341939290309, 6.645403452391245303 ),
 .UNSPECIFIED. ) 
 CURVE ( )  GEOMETRIC_REPRESENTATION_ITEM ( )  RATIONAL_B_SPLINE_CURVE ( ( 1.000000000000000000, 0.8120851936182301722, 0.8120851936182301722, 1.000000000000000000 ) ) 
 REPRESENTATION_ITEM ( '' )  );
#130898=DIRECTION ( 'NONE',  ( 1.000000000000000000, 0.000000000000000000, 0.000000000000000000 ) ) ;
#130899=CARTESIAN_POINT ( 'NONE',  ( -7.828169399223472880, -20.24070752338407075, 4.000000000000000000 ) ) ;
#130900=VECTOR ( 'NONE', #57270, 1000.000000000000000 ) ;
#130901=CARTESIAN_POINT ( 'NONE',  ( 65.99451991528749772, 28.92564299267984396, 4.000000000000000000 ) ) ;
#130902=DIRECTION ( 'NONE',  ( -0.7071067811865487940, 0.7071067811865463515, 0.000000000000000000 ) ) ;
#130903=EDGE_LOOP ( 'NONE', ( #13132, #103265, #67668, #81000 ) ) ;
#130904=DIRECTION ( 'NONE',  ( 1.000000000000000000, 0.000000000000000000, 0.000000000000000000 ) ) ;
#130905=VERTEX_POINT ( 'NONE', #272 ) ;
#130906=DIRECTION ( 'NONE',  ( 0.7071067811865487940, -0.7071067811865463515, 0.000000000000000000 ) ) ;
#130907=DIRECTION ( 'NONE',  ( -0.000000000000000000, 0.000000000000000000, 1.000000000000000000 ) ) ;
#130908=ORIENTED_EDGE ( 'NONE', *, *, #138064, .T. ) ;
#130912=CARTESIAN_POINT ( 'NONE',  ( -9.722814304570524868, -21.72500000000000497, 5.000000000000000000 ) ) ;
#130913=FACE_OUTER_BOUND ( 'NONE', #51252, .T. ) ;
#130914=CARTESIAN_POINT ( 'NONE',  ( -27.48921356237309155, -27.52281430457074762, 5.000000000000000000 ) ) ;
#130915=VERTEX_POINT ( 'NONE', #141711 ) ;
#130916=ORIENTED_EDGE ( 'NONE', *, *, #63346, .T. ) ;
#130918=PLANE ( 'NONE',  #95352 ) ;
#130919=CARTESIAN_POINT ( 'NONE',  ( -33.78162688292469795, 21.74787736706806740, 4.999607392498048419 ) ) ;
#130920=LINE ( 'NONE', #22112, #34355 ) ;
#130922=DIRECTION ( 'NONE',  ( -0.7071067811865486830, -0.7071067811865464625, 0.000000000000000000 ) ) ;
#130923=VECTOR ( 'NONE', #14116, 1000.000000000000000 ) ;
#130924=EDGE_CURVE ( 'NONE', #126257, #40492, #54007, .T. ) ;
#130926=EDGE_LOOP ( 'NONE', ( #58601, #83206, #45764 ) ) ;
#130927=VECTOR ( 'NONE', #119002, 1000.000000000000000 ) ;
#130928=CARTESIAN_POINT ( 'NONE',  ( 6.489213562373093325, -27.52281430457059841, 5.000000000000000000 ) ) ;
#130929=EDGE_CURVE ( 'NONE', #29058, #9428, #42415, .T. ) ;
#130930=DIRECTION ( 'NONE',  ( -0.7071067811865486830, -0.7071067811865464625, 0.000000000000000000 ) ) ;
#130933=EDGE_CURVE ( 'NONE', #45676, #46507, #22041, .T. ) ;
#130934=EDGE_CURVE ( 'NONE', #132567, #37221, #131538, .T. ) ;
#130935=CARTESIAN_POINT ( 'NONE',  ( -21.70612307739179769, 22.22500000000000142, 4.000000000000000000 ) ) ;
#130936=EDGE_LOOP ( 'NONE', ( #88532, #87981, #130668, #131815 ) ) ;
#130939=CARTESIAN_POINT ( 'NONE',  ( 2.510786437626908008, -27.52281430457053446, 5.000000000000000000 ) ) ;
#130941=CARTESIAN_POINT ( 'NONE',  ( 0.000000000000000000, 0.000000000000000000, 5.000000000000000000 ) ) ;
#130942=LINE ( 'NONE', #7692, #113681 ) ;
#130943=EDGE_CURVE ( 'NONE', #66659, #24466, #66296, .T. ) ;
#130944=DIRECTION ( 'NONE',  ( 0.3543493200069162685, -0.000000000000000000, -0.9351131265310288487 ) ) ;
#130945=ADVANCED_FACE ( 'NONE', ( #11139 ), #86627, .F. ) ;
#130950=FACE_OUTER_BOUND ( 'NONE', #112983, .T. ) ;
#130952=ORIENTED_EDGE ( 'NONE', *, *, #7377, .T. ) ;
#130953=EDGE_CURVE ( 'NONE', #128691, #3502, #132997, .T. ) ;
#130954=ORIENTED_EDGE ( 'NONE', *, *, #93425, .F. ) ;
#130956=VERTEX_POINT ( 'NONE', #44571 ) ;
#130957=CARTESIAN_POINT ( 'NONE',  ( -54.18398860626899705, 28.73617430169825226, 5.000000000000000000 ) ) ;
#130958=LINE ( 'NONE', #31630, #103586 ) ;
#130959=LINE ( 'NONE', #7708, #6343 ) ;
#130960=PLANE ( 'NONE',  #40953 ) ;
#130961=ORIENTED_EDGE ( 'NONE', *, *, #107708, .T. ) ;
#130962=EDGE_CURVE ( 'NONE', #44496, #94791, #98202, .T. ) ;
#130963=LINE ( 'NONE', #20736, #9830 ) ;
#130964=ORIENTED_EDGE ( 'NONE', *, *, #41060, .F. ) ;
#130965=DIRECTION ( 'NONE',  ( -0.7071067811865487940, 0.7071067811865463515, -0.000000000000000000 ) ) ;
#130967=EDGE_CURVE ( 'NONE', #28081, #124509, #143122, .T. ) ;
#130968=LINE ( 'NONE', #30941, #72503 ) ;
#130969=ORIENTED_EDGE ( 'NONE', *, *, #116236, .F. ) ;
#130970=ORIENTED_EDGE ( 'NONE', *, *, #118170, .T. ) ;
#130971=FACE_BOUND ( 'NONE', #95038, .T. ) ;
#130972=PLANE ( 'NONE',  #13067 ) ;
#130973=ADVANCED_FACE ( 'NONE', ( #75737 ), #119909, .F. ) ;
#130974=CARTESIAN_POINT ( 'NONE',  ( 42.29974487139158157, -27.71228299555235708, 4.000000000000000000 ) ) ;
#130975=DIRECTION ( 'NONE',  ( -0.7071067811865487940, 0.7071067811865463515, 0.000000000000000000 ) ) ;
#130976=EDGE_CURVE ( 'NONE', #17123, #68874, #32973, .T. ) ;
#130977=FACE_OUTER_BOUND ( 'NONE', #107016, .T. ) ;
#130978=DIRECTION ( 'NONE',  ( -0.7071067811865486830, -0.7071067811865464625, -0.000000000000000000 ) ) ;
#130980=EDGE_CURVE ( 'NONE', #56830, #142885, #20613, .T. ) ;
#130981=VECTOR ( 'NONE', #108407, 1000.000000000000000 ) ;
#130982=EDGE_LOOP ( 'NONE', ( #87771, #18010, #12928, #40915 ) ) ;
#130985=ORIENTED_EDGE ( 'NONE', *, *, #26273, .T. ) ;
#130986=ORIENTED_EDGE ( 'NONE', *, *, #91994, .F. ) ;
#130988=LINE ( 'NONE', #121502, #84815 ) ;
#130991=CARTESIAN_POINT ( 'NONE',  ( 27.18398860626900060, 28.73617430169806042, 5.000000000000000000 ) ) ;
#130992=CARTESIAN_POINT ( 'NONE',  ( -63.18398860626900415, 28.73617430169831621, 5.000000000000000000 ) ) ;
#130993=CARTESIAN_POINT ( 'NONE',  ( -10.49999999999992539, 1.466399257802250222, 5.000000000000000000 ) ) ;
#130994=DIRECTION ( 'NONE',  ( 0.7071067811865487940, -0.7071067811865463515, 0.000000000000000000 ) ) ;
#130995=CARTESIAN_POINT ( 'NONE',  ( 9.299744871391588674, -27.71228299555212971, 4.000000000000000000 ) ) ;
#130997=ORIENTED_EDGE ( 'NONE', *, *, #99618, .T. ) ;
#130998=CARTESIAN_POINT ( 'NONE',  ( -19.99806943317887331, -22.22500000000000142, 4.500000000000000888 ) ) ;
#131000=VERTEX_POINT ( 'NONE', #109048 ) ;
#131001=PLANE ( 'NONE',  #4139 ) ;
#131002=ORIENTED_EDGE ( 'NONE', *, *, #36055, .F. ) ;
#131006=AXIS2_PLACEMENT_3D ( 'NONE', #79452, #22140, #101859 ) ;
#131007=CARTESIAN_POINT ( 'NONE',  ( -0.1839886062690032631, 28.73617430169787568, 5.000000000000000000 ) ) ;
#131009=LINE ( 'NONE', #53431, #98033 ) ;
#131010=AXIS2_PLACEMENT_3D ( 'NONE', #22018, #22704, #132972 ) ;
#131011=EDGE_CURVE ( 'NONE', #123836, #141489, #87325, .T. ) ;
#131012=LINE ( 'NONE', #41853, #60592 ) ;
#131014=LINE ( 'NONE', #12768, #34957 ) ;
#131016=DIRECTION ( 'NONE',  ( -0.000000000000000000, 0.000000000000000000, 1.000000000000000000 ) ) ;
#131020=ORIENTED_EDGE ( 'NONE', *, *, #95599, .T. ) ;
#131021=ORIENTED_EDGE ( 'NONE', *, *, #32376, .T. ) ;
#131022=ORIENTED_EDGE ( 'NONE', *, *, #141966, .F. ) ;
#131024=EDGE_LOOP ( 'NONE', ( #134958, #3684, #66752 ) ) ;
#131025=CARTESIAN_POINT ( 'NONE',  ( -11.99451991528749417, 28.92564299267946382, 4.000000000000000000 ) ) ;
#131027=PLANE ( 'NONE',  #67214 ) ;
#131028=VERTEX_POINT ( 'NONE', #36507 ) ;
#131029=EDGE_CURVE ( 'NONE', #36667, #8819, #35106, .T. ) ;
#131030=CARTESIAN_POINT ( 'NONE',  ( -42.18398860626899705, 28.73617430169816700, 5.000000000000000000 ) ) ;
#131031=ORIENTED_EDGE ( 'NONE', *, *, #63525, .F. ) ;
#131033=CARTESIAN_POINT ( 'NONE',  ( 32.99999999999977973, -22.06887692260758271, 4.000000000000000000 ) ) ;
#131034=DIRECTION ( 'NONE',  ( 1.000000000000000000, 0.000000000000000000, 0.000000000000000000 ) ) ;
#131035=EDGE_CURVE ( 'NONE', #121873, #13630, #59026, .T. ) ;
#131037=EDGE_LOOP ( 'NONE', ( #74120, #139115, #36102, #109044 ) ) ;
#131038=ORIENTED_EDGE ( 'NONE', *, *, #70708, .F. ) ;
#131039=ORIENTED_EDGE ( 'NONE', *, *, #72659, .F. ) ;
#131042=CARTESIAN_POINT ( 'NONE',  ( -8.999999999999934275, -21.84840872380825516, 2.849755605029586469 ) ) ;
#131043=EDGE_CURVE ( 'NONE', #92938, #97574, #102499, .T. ) ;
#131046=CARTESIAN_POINT ( 'NONE',  ( 29.99999999999980105, -22.06887692260758982, 4.000000000000000000 ) ) ;
#131047=LINE ( 'NONE', #31731, #113735 ) ;
#131049=LINE ( 'NONE', #118728, #136664 ) ;
#131050=ORIENTED_EDGE ( 'NONE', *, *, #33738, .F. ) ;
#131051=ADVANCED_FACE ( 'NONE', ( #3147 ), #80747, .F. ) ;
#131053=ORIENTED_EDGE ( 'NONE', *, *, #106699, .F. ) ;
#131054=CARTESIAN_POINT ( 'NONE',  ( -25.49999999999982236, -13.91253812416061031, 4.000000000000000000 ) ) ;
#131057=CARTESIAN_POINT ( 'NONE',  ( 21.66846741159843859, -18.74070752338408852, 20.73178291233846338 ) ) ;
#131058=ORIENTED_EDGE ( 'NONE', *, *, #92265, .T. ) ;
#131059=EDGE_LOOP ( 'NONE', ( #93563, #14443, #30104, #5792 ) ) ;
#131060=LINE ( 'NONE', #65848, #62892 ) ;
#131061=VERTEX_POINT ( 'NONE', #135140 ) ;
#131062=( BOUNDED_CURVE ( )  B_SPLINE_CURVE ( 3, ( #10778, #32580, #85492, #87659 ),
 .UNSPECIFIED., .F., .T. ) 
 B_SPLINE_CURVE_WITH_KNOTS ( ( 4, 4 ),
 ( 5.106027341939297415, 6.645403452391245303 ),
 .UNSPECIFIED. ) 
 CURVE ( )  GEOMETRIC_REPRESENTATION_ITEM ( )  RATIONAL_B_SPLINE_CURVE ( ( 1.000000000000000000, 0.8120851936182316155, 0.8120851936182316155, 1.000000000000000000 ) ) 
 REPRESENTATION_ITEM ( '' )  );
#131065=CARTESIAN_POINT ( 'NONE',  ( 14.51078643762690490, -27.52281430457045275, 5.000000000000000000 ) ) ;
#131066=DIRECTION ( 'NONE',  ( -0.3543493200069162685, -0.000000000000000000, -0.9351131265310288487 ) ) ;
#131067=VECTOR ( 'NONE', #45222, 1000.000000000000000 ) ;
#131068=LINE ( 'NONE', #52081, #109277 ) ;
#131070=ADVANCED_FACE ( 'NONE', ( #16139 ), #101033, .F. ) ;
#131071=CARTESIAN_POINT ( 'NONE',  ( -26.99999999999981526, 7.007997736742422212, -8.085015511992175163 ) ) ;
#131074=CARTESIAN_POINT ( 'NONE',  ( -20.41126436577413727, 22.22500000000000142, -0.4997969837368500534 ) ) ;
#131075=CARTESIAN_POINT ( 'NONE',  ( 18.48921356237309510, -27.52281430457068367, 5.000000000000000000 ) ) ;
#131076=VERTEX_POINT ( 'NONE', #69153 ) ;
#131077=EDGE_CURVE ( 'NONE', #68534, #106183, #136516, .T. ) ;
#131078=ORIENTED_EDGE ( 'NONE', *, *, #143521, .F. ) ;
#131080=FACE_OUTER_BOUND ( 'NONE', #53116, .T. ) ;
#131081=EDGE_LOOP ( 'NONE', ( #67266, #142289, #24526, #43562 ) ) ;
#131082=VECTOR ( 'NONE', #2477, 1000.000000000000000 ) ;
#131083=DIRECTION ( 'NONE',  ( -0.000000000000000000, 0.3543493200069153248, 0.9351131265310292928 ) ) ;
#131087=EDGE_LOOP ( 'NONE', ( #113680, #82721, #101751, #65430, #51448 ) ) ;
#131088=EDGE_CURVE ( 'NONE', #32610, #136433, #112638, .T. ) ;
#131089=CARTESIAN_POINT ( 'NONE',  ( -34.92500000000001137, 21.72500000000000142, 5.000000000000000000 ) ) ;
#131090=PLANE ( 'NONE',  #141362 ) ;
#131091=CARTESIAN_POINT ( 'NONE',  ( 24.18398860626899705, 28.73617430169804265, 5.000000000000000000 ) ) ;
#131092=VECTOR ( 'NONE', #90652, 1000.000000000000227 ) ;
#131093=EDGE_CURVE ( 'NONE', #105033, #131076, #114061, .T. ) ;
#131094=EDGE_CURVE ( 'NONE', #101036, #40900, #59708, .T. ) ;
#131095=DIRECTION ( 'NONE',  ( -0.000000000000000000, 0.000000000000000000, 1.000000000000000000 ) ) ;
#131097=ORIENTED_EDGE ( 'NONE', *, *, #48877, .F. ) ;
#131101=CARTESIAN_POINT ( 'NONE',  ( -26.99999999999980460, -12.41253812416063163, 4.000000000000000000 ) ) ;
#131103=CARTESIAN_POINT ( 'NONE',  ( 77.99451991528749772, 28.92564299267992567, 4.000000000000000000 ) ) ;
#131105=ORIENTED_EDGE ( 'NONE', *, *, #13047, .T. ) ;
#131106=EDGE_LOOP ( 'NONE', ( #102755, #118509, #21236, #21517 ) ) ;
#131107=ORIENTED_EDGE ( 'NONE', *, *, #19930, .T. ) ;
#131108=VECTOR ( 'NONE', #81913, 1000.000000000000227 ) ;
#131110=ORIENTED_EDGE ( 'NONE', *, *, #64502, .T. ) ;
#131111=EDGE_CURVE ( 'NONE', #49923, #91902, #60431, .T. ) ;
#131112=AXIS2_PLACEMENT_3D ( 'NONE', #87765, #75473, #21793 ) ;
#131114=VECTOR ( 'NONE', #52940, 1000.000000000000000 ) ;
#131116=ORIENTED_EDGE ( 'NONE', *, *, #17682, .T. ) ;
#131117=EDGE_CURVE ( 'NONE', #111746, #133264, #96553, .T. ) ;
#131118=DIRECTION ( 'NONE',  ( 0.6830127018922181881, 0.6830127018922202975, -0.2588190451025214056 ) ) ;
#131121=VERTEX_POINT ( 'NONE', #140792 ) ;
#131124=VERTEX_POINT ( 'NONE', #6681 ) ;
#131126=ORIENTED_EDGE ( 'NONE', *, *, #56529, .T. ) ;
#131127=PLANE ( 'NONE',  #32985 ) ;
#131128=CARTESIAN_POINT ( 'NONE',  ( 6.604862331875168913, 21.75929247661549937, 21.32995629748185351 ) ) ;
#131130=CARTESIAN_POINT ( 'NONE',  ( 11.67183060077639212, -15.74070752338412760, 4.000000000000000000 ) ) ;
#131131=EDGE_CURVE ( 'NONE', #21371, #131987, #74877, .T. ) ;
#131134=EDGE_CURVE ( 'NONE', #71156, #84656, #85698, .T. ) ;
#131136=ORIENTED_EDGE ( 'NONE', *, *, #118380, .T. ) ;
#131138=LINE ( 'NONE', #110077, #43345 ) ;
#131139=VERTEX_POINT ( 'NONE', #128521 ) ;
#131140=VERTEX_POINT ( 'NONE', #39380 ) ;
#131141=VECTOR ( 'NONE', #55678, 1000.000000000000227 ) ;
#131142=LINE ( 'NONE', #20207, #33553 ) ;
#131143=ORIENTED_EDGE ( 'NONE', *, *, #68404, .T. ) ;
#131144=DIRECTION ( 'NONE',  ( -0.000000000000000000, 0.000000000000000000, 1.000000000000000000 ) ) ;
#131147=VECTOR ( 'NONE', #66356, 1000.000000000000000 ) ;
#131148=CARTESIAN_POINT ( 'NONE',  ( -21.48921356237309155, -27.52281430457070499, 5.000000000000000000 ) ) ;
#131149=ORIENTED_EDGE ( 'NONE', *, *, #89907, .T. ) ;
#131150=DIRECTION ( 'NONE',  ( -0.7071067811865487940, 0.7071067811865463515, 0.000000000000000000 ) ) ;
#131151=ORIENTED_EDGE ( 'NONE', *, *, #118601, .T. ) ;
#131152=LINE ( 'NONE', #63074, #71294 ) ;
#131153=ORIENTED_EDGE ( 'NONE', *, *, #12082, .T. ) ;
#131155=ORIENTED_EDGE ( 'NONE', *, *, #80303, .T. ) ;
#131156=DIRECTION ( 'NONE',  ( -0.7071067811865487940, 0.7071067811865463515, 0.000000000000000000 ) ) ;
#131157=ORIENTED_EDGE ( 'NONE', *, *, #33885, .T. ) ;
#131158=ORIENTED_EDGE ( 'NONE', *, *, #15946, .F. ) ;
#131159=ORIENTED_EDGE ( 'NONE', *, *, #67809, .F. ) ;
#131160=VECTOR ( 'NONE', #32954, 1000.000000000000227 ) ;
#131161=CARTESIAN_POINT ( 'NONE',  ( 14.54487008052911534, -0.7407075233842805861, 4.335043535661647240 ) ) ;
#131165=LINE ( 'NONE', #142069, #54398 ) ;
#131166=ADVANCED_FACE ( 'NONE', ( #19031 ), #119051, .F. ) ;
#131167=DIRECTION ( 'NONE',  ( -0.7071067811865486830, -0.7071067811865464625, -0.000000000000000000 ) ) ;
#131168=DIRECTION ( 'NONE',  ( -0.7071067811865487940, 0.7071067811865463515, -0.000000000000000000 ) ) ;
#131169=CARTESIAN_POINT ( 'NONE',  ( 34.49999999999975131, 22.21934299833216642, 4.348028800457638177 ) ) ;
#131170=PLANE ( 'NONE',  #133907 ) ;
#131171=LINE ( 'NONE', #64489, #36692 ) ;
#131173=VECTOR ( 'NONE', #31664, 1000.000000000000000 ) ;
#131174=ORIENTED_EDGE ( 'NONE', *, *, #38660, .T. ) ;
#131175=ORIENTED_EDGE ( 'NONE', *, *, #138417, .T. ) ;
#131176=VERTEX_POINT ( 'NONE', #73430 ) ;
#131178=ORIENTED_EDGE ( 'NONE', *, *, #23020, .T. ) ;
#131179=ADVANCED_FACE ( 'NONE', ( #84325 ), #137973, .F. ) ;
#131180=ORIENTED_EDGE ( 'NONE', *, *, #28759, .F. ) ;
#131181=DIRECTION ( 'NONE',  ( 0.7071067811865486830, -0.7071067811865464625, -0.000000000000000000 ) ) ;
#131182=DIRECTION ( 'NONE',  ( 0.7071067811865487940, 0.7071067811865463515, 0.000000000000000000 ) ) ;
#131183=VECTOR ( 'NONE', #140224, 1000.000000000000000 ) ;
#131184=EDGE_CURVE ( 'NONE', #54005, #132339, #72028, .T. ) ;
#131186=DIRECTION ( 'NONE',  ( -0.6830127018922180770, -0.6830127018922204085, -0.2588190451025213501 ) ) ;
#131187=ORIENTED_EDGE ( 'NONE', *, *, #59822, .F. ) ;
#131188=DIRECTION ( 'NONE',  ( -0.7071067811865486830, -0.7071067811865464625, 0.000000000000000000 ) ) ;
#131189=ORIENTED_EDGE ( 'NONE', *, *, #31581, .F. ) ;
#131190=VECTOR ( 'NONE', #756, 1000.000000000000227 ) ;
#131191=VECTOR ( 'NONE', #57343, 1000.000000000000000 ) ;
#131192=PLANE ( 'NONE',  #35256 ) ;
#131193=ADVANCED_FACE ( 'NONE', ( #117594 ), #95872, .F. ) ;
#131195=CARTESIAN_POINT ( 'NONE',  ( 34.92499999999998295, 5.816654386410395894, 4.500000000000000888 ) ) ;
#131196=AXIS2_PLACEMENT_3D ( 'NONE', #82800, #38566, #101666 ) ;
#131204=ORIENTED_EDGE ( 'NONE', *, *, #98369, .T. ) ;
#131205=ORIENTED_EDGE ( 'NONE', *, *, #41097, .T. ) ;
#131207=ORIENTED_EDGE ( 'NONE', *, *, #74400, .F. ) ;
#131208=CARTESIAN_POINT ( 'NONE',  ( -2.526639036357837487, -5.240707523384232402, 16.25846745537495153 ) ) ;
#131209=VECTOR ( 'NONE', #49962, 999.9999999999998863 ) ;
#131210=CARTESIAN_POINT ( 'NONE',  ( -11.99999999999991651, -3.033600742197707145, 5.000000000000000000 ) ) ;
#131212=EDGE_LOOP ( 'NONE', ( #88975, #4289, #74820, #95531 ) ) ;
#131213=DIRECTION ( 'NONE',  ( -0.7071067811865486830, -0.7071067811865464625, 0.000000000000000000 ) ) ;
#131214=ADVANCED_FACE ( 'NONE', ( #77711 ), #120442, .F. ) ;
#131215=DIRECTION ( 'NONE',  ( 0.000000000000000000, -0.3543493200069152138, 0.9351131265310292928 ) ) ;
#131216=LINE ( 'NONE', #118162, #76942 ) ;
#131217=ORIENTED_EDGE ( 'NONE', *, *, #74245, .T. ) ;
#131219=EDGE_CURVE ( 'NONE', #63455, #60759, #9555, .T. ) ;
#131220=CARTESIAN_POINT ( 'NONE',  ( -14.29289321881335084, -12.74070752338415247, 5.000000000000000000 ) ) ;
#131222=DIRECTION ( 'NONE',  ( -0.7071067811865486830, -0.7071067811865464625, -0.000000000000000000 ) ) ;
#131223=ORIENTED_EDGE ( 'NONE', *, *, #140215, .T. ) ;
#131224=ORIENTED_EDGE ( 'NONE', *, *, #36486, .T. ) ;
#131225=DIRECTION ( 'NONE',  ( 0.7071067811865486830, -0.7071067811865464625, -0.000000000000000000 ) ) ;
#131226=CARTESIAN_POINT ( 'NONE',  ( 34.92499999999998295, -21.72500000000000142, 5.000000000000000000 ) ) ;
#131227=EDGE_CURVE ( 'NONE', #26091, #135979, #55978, .T. ) ;
#131228=ORIENTED_EDGE ( 'NONE', *, *, #25740, .T. ) ;
#131230=LINE ( 'NONE', #87728, #33630 ) ;
#131231=AXIS2_PLACEMENT_3D ( 'NONE', #30272, #52723, #63647 ) ;
#131232=DIRECTION ( 'NONE',  ( 0.7071067811865486830, -0.7071067811865464625, -0.000000000000000000 ) ) ;
#131233=PLANE ( 'NONE',  #76275 ) ;
#131234=CARTESIAN_POINT ( 'NONE',  ( -11.67183060077638856, -12.74070752338415602, 4.000000000000000000 ) ) ;
#131235=DIRECTION ( 'NONE',  ( 0.7071067811865487940, 0.7071067811865463515, -0.000000000000000000 ) ) ;
#131236=LINE ( 'NONE', #1404, #56512 ) ;
#131237=EDGE_CURVE ( 'NONE', #103116, #44686, #8811, .T. ) ;
#131239=CARTESIAN_POINT ( 'NONE',  ( -26.22995720542188991, 21.73644205237998150, 5.000000000000000888 ) ) ;
#131240=FACE_OUTER_BOUND ( 'NONE', #68161, .T. ) ;
#131241=AXIS2_PLACEMENT_3D ( 'NONE', #38393, #82609, #39846 ) ;
#131242=DIRECTION ( 'NONE',  ( -0.000000000000000000, -0.3543493200069152693, 0.9351131265310292928 ) ) ;
#131243=DIRECTION ( 'NONE',  ( 0.7071067811865487940, 0.7071067811865463515, 0.000000000000000000 ) ) ;
#131244=CARTESIAN_POINT ( 'NONE',  ( -26.20710678118635428, -17.24070752338410273, 5.000000000000000000 ) ) ;
#131245=VERTEX_POINT ( 'NONE', #31348 ) ;
#131252=EDGE_CURVE ( 'NONE', #126555, #60629, #45112, .T. ) ;
#131253=ORIENTED_EDGE ( 'NONE', *, *, #72386, .T. ) ;
#131255=DIRECTION ( 'NONE',  ( -0.000000000000000000, 0.000000000000000000, 1.000000000000000000 ) ) ;
#131257=ORIENTED_EDGE ( 'NONE', *, *, #142063, .T. ) ;
#131258=LINE ( 'NONE', #87754, #64893 ) ;
#131259=EDGE_CURVE ( 'NONE', #91901, #26770, #53070, .T. ) ;
#131260=LINE ( 'NONE', #120335, #60376 ) ;
#131262=VECTOR ( 'NONE', #76054, 1000.000000000000000 ) ;
#131266=CARTESIAN_POINT ( 'NONE',  ( 15.79333936457837062, 21.75929247661549937, 4.998822639870715179 ) ) ;
#131267=CARTESIAN_POINT ( 'NONE',  ( 24.30132219248945447, 6.014229859109025966, 4.331046227559734341 ) ) ;
#131268=CARTESIAN_POINT ( 'NONE',  ( -75.18398860626899705, 28.73617430169839793, 5.000000000000000000 ) ) ;
#131269=DIRECTION ( 'NONE',  ( -0.7071067811865487940, 0.7071067811865463515, -0.000000000000000000 ) ) ;
#131272=FACE_OUTER_BOUND ( 'NONE', #125236, .T. ) ;
#131274=EDGE_LOOP ( 'NONE', ( #65562, #105138, #102091, #103854 ) ) ;
#131276=VECTOR ( 'NONE', #46858, 1000.000000000000000 ) ;
#131278=EDGE_CURVE ( 'NONE', #108755, #101225, #98718, .T. ) ;
#131279=PLANE ( 'NONE',  #15884 ) ;
#131280=DIRECTION ( 'NONE',  ( 0.000000000000000000, 0.000000000000000000, -1.000000000000000000 ) ) ;
#131282=EDGE_CURVE ( 'NONE', #71076, #47430, #87860, .T. ) ;
#131283=DIRECTION ( 'NONE',  ( 0.3543493200069162685, -0.000000000000000000, -0.9351131265310288487 ) ) ;
#131284=DIRECTION ( 'NONE',  ( -0.3543493200069162685, -0.000000000000000000, -0.9351131265310288487 ) ) ;
#131287=EDGE_LOOP ( 'NONE', ( #102638, #129997, #27436, #55037 ) ) ;
#131288=ORIENTED_EDGE ( 'NONE', *, *, #125978, .F. ) ;
#131289=CARTESIAN_POINT ( 'NONE',  ( -25.49999999999982236, -2.568876922607784774, 4.000000000000000000 ) ) ;
#131290=CARTESIAN_POINT ( 'NONE',  ( 30.18398860626900060, 28.73617430169808173, 5.000000000000000000 ) ) ;
#131291=LINE ( 'NONE', #122351, #113560 ) ;
#131292=CARTESIAN_POINT ( 'NONE',  ( -21.29974487139158512, -27.71228299555221142, 4.000000000000000000 ) ) ;
#131293=ORIENTED_EDGE ( 'NONE', *, *, #71240, .T. ) ;
#131296=ORIENTED_EDGE ( 'NONE', *, *, #104845, .F. ) ;
#131297=DIRECTION ( 'NONE',  ( 0.7071067811865487940, 0.7071067811865463515, 0.000000000000000000 ) ) ;
#131298=CARTESIAN_POINT ( 'NONE',  ( -35.99451991528749772, 28.92564299267963079, 4.000000000000000000 ) ) ;
#131299=CARTESIAN_POINT ( 'NONE',  ( 33.48921356237309510, -27.52281430457078670, 5.000000000000000000 ) ) ;
#131300=DIRECTION ( 'NONE',  ( -0.6830127018922181881, 0.6830127018922202975, -0.2588190451025214056 ) ) ;
#131301=VECTOR ( 'NONE', #66251, 1000.000000000000000 ) ;
#131302=VECTOR ( 'NONE', #15047, 1000.000000000000000 ) ;
#131303=ADVANCED_FACE ( 'NONE', ( #21171 ), #78419, .F. ) ;
#131304=VECTOR ( 'NONE', #133436, 999.9999999999998863 ) ;
#131306=ORIENTED_EDGE ( 'NONE', *, *, #88553, .T. ) ;
#131307=VECTOR ( 'NONE', #45493, 999.9999999999998863 ) ;
#131308=DIRECTION ( 'NONE',  ( -0.6830127018922181881, 0.6830127018922202975, -0.2588190451025214056 ) ) ;
#131309=EDGE_LOOP ( 'NONE', ( #54785, #51014, #108375, #138217 ) ) ;
#131313=EDGE_CURVE ( 'NONE', #2249, #67897, #32054, .T. ) ;
#131314=CARTESIAN_POINT ( 'NONE',  ( -34.49999999999976552, 1.464255608400471642, 4.994342998332163219 ) ) ;
#131315=PLANE ( 'NONE',  #60764 ) ;
#131316=ORIENTED_EDGE ( 'NONE', *, *, #134896, .F. ) ;
#131317=CARTESIAN_POINT ( 'NONE',  ( 2.999999999999981792, 14.87792677143809073, -11.06722581663439264 ) ) ;
#131318=PLANE ( 'NONE',  #32043 ) ;
#131319=( BOUNDED_CURVE ( )  B_SPLINE_CURVE ( 3, ( #12265, #89138, #101417, #102867 ),
 .UNSPECIFIED., .F., .F. ) 
 B_SPLINE_CURVE_WITH_KNOTS ( ( 4, 4 ),
 ( 4.350170835173029715, 4.500739107949200957 ),
 .UNSPECIFIED. ) 
 CURVE ( )  GEOMETRIC_REPRESENTATION_ITEM ( )  RATIONAL_B_SPLINE_CURVE ( ( 1.000000000000000000, 0.9981116584018959736, 0.9981116584018959736, 1.000000000000000000 ) ) 
 REPRESENTATION_ITEM ( '' )  );
#131320=CARTESIAN_POINT ( 'NONE',  ( 22.77149322861322034, 20.25929247661551003, 7.808871592221821700 ) ) ;
#131321=FACE_BOUND ( 'NONE', #11627, .T. ) ;
#131322=EDGE_LOOP ( 'NONE', ( #14644, #87842, #52574, #138102 ) ) ;
#131323=EDGE_CURVE ( 'NONE', #38880, #73106, #10973, .T. ) ;
#131324=DIRECTION ( 'NONE',  ( -0.6830127018922181881, 0.6830127018922202975, -0.2588190451025214056 ) ) ;
#131325=CARTESIAN_POINT ( 'NONE',  ( -17.70025512860841488, -27.71228299555193786, 4.000000000000000000 ) ) ;
#131326=FACE_OUTER_BOUND ( 'NONE', #137419, .T. ) ;
#131327=ORIENTED_EDGE ( 'NONE', *, *, #62906, .F. ) ;
#131328=CARTESIAN_POINT ( 'NONE',  ( -14.99999999999989519, 11.96639925780214675, 5.000000000000000000 ) ) ;
#131329=ORIENTED_EDGE ( 'NONE', *, *, #39321, .F. ) ;
#131330=AXIS2_PLACEMENT_3D ( 'NONE', #29020, #73254, #27570 ) ;
#131332=CARTESIAN_POINT ( 'NONE',  ( 10.49999999999992895, -19.91253812416055169, 4.000000000000000000 ) ) ;
#131333=ORIENTED_EDGE ( 'NONE', *, *, #135003, .F. ) ;
#131335=AXIS2_PLACEMENT_3D ( 'NONE', #71673, #94806, #139069 ) ;
#131336=ORIENTED_EDGE ( 'NONE', *, *, #140735, .F. ) ;
#131337=DIRECTION ( 'NONE',  ( -0.7071067811865487940, 0.7071067811865463515, 0.000000000000000000 ) ) ;
#131338=ORIENTED_EDGE ( 'NONE', *, *, #74200, .F. ) ;
#131339=CARTESIAN_POINT ( 'NONE',  ( -24.32816939922335919, 17.25929247661554555, 4.000000000000000000 ) ) ;
#131340=LINE ( 'NONE', #142240, #46457 ) ;
#131343=CARTESIAN_POINT ( 'NONE',  ( -29.99999999999979039, -8.151047557385094677, -8.977947279169729455 ) ) ;
#131344=AXIS2_PLACEMENT_3D ( 'NONE', #2452, #11911, #57604 ) ;
#131345=CARTESIAN_POINT ( 'NONE',  ( -63.18398860626900415, 28.73617430169831621, 5.000000000000000000 ) ) ;
#131346=DIRECTION ( 'NONE',  ( 0.000000000000000000, 0.000000000000000000, -1.000000000000000000 ) ) ;
#131347=DIRECTION ( 'NONE',  ( 0.7071067811865487940, 0.7071067811865463515, 0.000000000000000000 ) ) ;
#131349=DIRECTION ( 'NONE',  ( 0.6830127018922181881, 0.6830127018922202975, -0.2588190451025214056 ) ) ;
#131350=EDGE_LOOP ( 'NONE', ( #118012, #2266, #63754, #44440 ) ) ;
#131351=EDGE_CURVE ( 'NONE', #104048, #78195, #21880, .T. ) ;
#131352=VECTOR ( 'NONE', #67262, 1000.000000000000000 ) ;
#131354=ORIENTED_EDGE ( 'NONE', *, *, #72353, .F. ) ;
#131355=CARTESIAN_POINT ( 'NONE',  ( 11.70025512860841133, -27.71228299555198049, 4.000000000000000000 ) ) ;
#131356=DIRECTION ( 'NONE',  ( -0.7071067811865486830, -0.7071067811865464625, 0.000000000000000000 ) ) ;
#131357=ORIENTED_EDGE ( 'NONE', *, *, #89955, .F. ) ;
#131358=EDGE_CURVE ( 'NONE', #27120, #27213, #64690, .T. ) ;
#131360=CARTESIAN_POINT ( 'NONE',  ( 24.18398860626899705, 28.73617430169804265, 5.000000000000000000 ) ) ;
#131361=DIRECTION ( 'NONE',  ( 0.7071067811865487940, 0.7071067811865463515, 0.000000000000000000 ) ) ;
#131362=VECTOR ( 'NONE', #49155, 1000.000000000000000 ) ;
#131363=ADVANCED_FACE ( 'NONE', ( #44390 ), #97265, .F. ) ;
#131365=DIRECTION ( 'NONE',  ( 1.000000000000000000, 0.000000000000000000, 0.000000000000000000 ) ) ;
#131367=CARTESIAN_POINT ( 'NONE',  ( 12.79289321881337393, -11.24070752338416845, 5.000000000000000000 ) ) ;
#131369=ADVANCED_FACE ( 'NONE', ( #4342 ), #123369, .F. ) ;
#131370=EDGE_CURVE ( 'NONE', #1453, #38684, #55948, .T. ) ;
#131372=LINE ( 'NONE', #75571, #66969 ) ;
#131373=ADVANCED_FACE ( 'NONE', ( #122616 ), #124060, .T. ) ;
#131374=ORIENTED_EDGE ( 'NONE', *, *, #11517, .F. ) ;
#131376=VECTOR ( 'NONE', #112429, 999.9999999999998863 ) ;
#131378=EDGE_CURVE ( 'NONE', #132753, #105598, #135547, .T. ) ;
#131379=CARTESIAN_POINT ( 'NONE',  ( 23.66989781452720365, 17.25929247661554555, 19.83885114516066039 ) ) ;
#131380=LINE ( 'NONE', #40804, #35730 ) ;
#131381=DIRECTION ( 'NONE',  ( 0.7071067811865487940, -0.7071067811865463515, 0.000000000000000000 ) ) ;
#131382=ORIENTED_EDGE ( 'NONE', *, *, #106, .T. ) ;
#131383=FACE_OUTER_BOUND ( 'NONE', #1750, .T. ) ;
#131385=EDGE_CURVE ( 'NONE', #43329, #110223, #56707, .T. ) ;
#131386=LINE ( 'NONE', #120454, #116821 ) ;
#131387=LINE ( 'NONE', #66146, #137271 ) ;
#131388=DIRECTION ( 'NONE',  ( -0.7071067811865486830, -0.7071067811865464625, 0.000000000000000000 ) ) ;
#131389=ORIENTED_EDGE ( 'NONE', *, *, #30229, .T. ) ;
#131391=VECTOR ( 'NONE', #69223, 1000.000000000000000 ) ;
#131392=FACE_OUTER_BOUND ( 'NONE', #126136, .T. ) ;
#131393=CARTESIAN_POINT ( 'NONE',  ( -1.171830600776458509, -2.240707523384264377, 4.000000000000000000 ) ) ;
#131394=EDGE_LOOP ( 'NONE', ( #120570, #105721, #16646, #6118 ) ) ;
#131395=CARTESIAN_POINT ( 'NONE',  ( -4.499999999999962697, 9.052185695429074030, 5.000000000000000000 ) ) ;
#131397=CARTESIAN_POINT ( 'NONE',  ( -34.49999999999975131, -17.91344420646045421, 1.358650452708383138 ) ) ;
#131398=ORIENTED_EDGE ( 'NONE', *, *, #126904, .F. ) ;
#131399=EDGE_CURVE ( 'NONE', #62769, #98772, #36343, .T. ) ;
#131400=VECTOR ( 'NONE', #43958, 1000.000000000000000 ) ;
#131401=DIRECTION ( 'NONE',  ( 0.7071067811865486830, -0.7071067811865464625, -0.000000000000000000 ) ) ;
#131402=CARTESIAN_POINT ( 'NONE',  ( 0.1839886062690032631, 28.73617430169787568, 5.000000000000000000 ) ) ;
#131404=ORIENTED_EDGE ( 'NONE', *, *, #103539, .T. ) ;
#131405=LINE ( 'NONE', #42982, #114323 ) ;
#131406=DIRECTION ( 'NONE',  ( 0.3543493200069163240, -0.000000000000000000, -0.9351131265310288487 ) ) ;
#131407=EDGE_CURVE ( 'NONE', #132567, #131487, #101573, .T. ) ;
#131408=AXIS2_PLACEMENT_3D ( 'NONE', #118187, #52935, #74745 ) ;
#131409=ORIENTED_EDGE ( 'NONE', *, *, #142272, .T. ) ;
#131411=LINE ( 'NONE', #32827, #101507 ) ;
#131412=VECTOR ( 'NONE', #6962, 1000.000000000000000 ) ;
#131415=EDGE_LOOP ( 'NONE', ( #29504, #62239, #133567, #59847 ) ) ;
#131416=CARTESIAN_POINT ( 'NONE',  ( -57.18398860626899705, 28.73617430169827358, 5.000000000000000000 ) ) ;
#131417=CARTESIAN_POINT ( 'NONE',  ( 42.29974487139158157, -27.71228299555235708, 4.000000000000000000 ) ) ;
#131418=CARTESIAN_POINT ( 'NONE',  ( -24.48921356237309510, -27.52281430457072631, 5.000000000000000000 ) ) ;
#131419=AXIS2_PLACEMENT_3D ( 'NONE', #54131, #142543, #51963 ) ;
#131420=CARTESIAN_POINT ( 'NONE',  ( -14.99451991528749595, 28.92564299267948513, 4.000000000000000000 ) ) ;
#131422=DIRECTION ( 'NONE',  ( 0.7071067811865487940, 0.7071067811865463515, 0.000000000000000000 ) ) ;
#131423=ORIENTED_EDGE ( 'NONE', *, *, #50499, .F. ) ;
#131424=ORIENTED_EDGE ( 'NONE', *, *, #65527, .F. ) ;
#131425=EDGE_CURVE ( 'NONE', #35489, #11869, #79167, .T. ) ;
#131426=EDGE_LOOP ( 'NONE', ( #4332, #115547, #8743, #7722 ) ) ;
#131427=EDGE_CURVE ( 'NONE', #133121, #82135, #13123, .T. ) ;
#131429=LINE ( 'NONE', #54591, #64096 ) ;
#131430=LINE ( 'NONE', #74929, #87834 ) ;
#131433=LINE ( 'NONE', #21232, #13823 ) ;
#131434=CARTESIAN_POINT ( 'NONE',  ( -15.32816939922341959, -21.74070752338406365, 4.000000000000000000 ) ) ;
#131438=ORIENTED_EDGE ( 'NONE', *, *, #15984, .F. ) ;
#131439=LINE ( 'NONE', #32118, #102022 ) ;
#131441=VECTOR ( 'NONE', #48831, 1000.000000000000000 ) ;
#131442=LINE ( 'NONE', #85067, #98169 ) ;
#131443=DIRECTION ( 'NONE',  ( 0.7071067811865486830, -0.7071067811865464625, -0.000000000000000000 ) ) ;
#131444=PLANE ( 'NONE',  #123747 ) ;
#131445=DIRECTION ( 'NONE',  ( -0.6830127018922180770, -0.6830127018922204085, -0.2588190451025213501 ) ) ;
#131446=DIRECTION ( 'NONE',  ( -0.6830127018922181881, 0.6830127018922202975, -0.2588190451025214056 ) ) ;
#131449=CARTESIAN_POINT ( 'NONE',  ( -15.18398860626900237, 28.73617430169797871, 5.000000000000000000 ) ) ;
#131450=ORIENTED_EDGE ( 'NONE', *, *, #21329, .T. ) ;
#131451=VERTEX_POINT ( 'NONE', #37041 ) ;
#131454=LINE ( 'NONE', #111660, #109488 ) ;
#131455=ADVANCED_FACE ( 'NONE', ( #80571 ), #2237, .F. ) ;
#131456=LINE ( 'NONE', #120530, #27730 ) ;
#131457=DIRECTION ( 'NONE',  ( -0.6830127018922180770, -0.6830127018922204085, -0.2588190451025213501 ) ) ;
#131458=EDGE_LOOP ( 'NONE', ( #51604, #56763, #44168, #23535 ) ) ;
#131460=DIRECTION ( 'NONE',  ( 0.3543493200069162685, -0.000000000000000000, -0.9351131265310288487 ) ) ;
#131462=EDGE_CURVE ( 'NONE', #116321, #2713, #58859, .T. ) ;
#131463=ORIENTED_EDGE ( 'NONE', *, *, #70324, .F. ) ;
#131464=CARTESIAN_POINT ( 'NONE',  ( -32.99999999999975842, 2.587461875839218273, 4.000000000000000000 ) ) ;
#131465=ORIENTED_EDGE ( 'NONE', *, *, #68544, .F. ) ;
#131466=ORIENTED_EDGE ( 'NONE', *, *, #13972, .F. ) ;
#131467=DIRECTION ( 'NONE',  ( -0.6830127018922181881, 0.6830127018922202975, -0.2588190451025214056 ) ) ;
#131469=LINE ( 'NONE', #140202, #136865 ) ;
#131470=DIRECTION ( 'NONE',  ( -0.6830127018922181881, 0.6830127018922202975, -0.2588190451025214056 ) ) ;
#131471=VERTEX_POINT ( 'NONE', #2975 ) ;
#131473=LINE ( 'NONE', #8218, #4787 ) ;
#131475=ORIENTED_EDGE ( 'NONE', *, *, #65362, .T. ) ;
#131477=LINE ( 'NONE', #19834, #94751 ) ;
#131479=EDGE_CURVE ( 'NONE', #69258, #129709, #50431, .T. ) ;
#131480=ORIENTED_EDGE ( 'NONE', *, *, #121577, .F. ) ;
#131481=AXIS2_PLACEMENT_3D ( 'NONE', #106161, #115589, #40261 ) ;
#131484=DIRECTION ( 'NONE',  ( 0.7071067811865487940, 0.7071067811865463515, 0.000000000000000000 ) ) ;
#131485=LINE ( 'NONE', #68405, #29259 ) ;
#131486=DIRECTION ( 'NONE',  ( -0.7071067811865486830, -0.7071067811865464625, 0.000000000000000000 ) ) ;
#131487=VERTEX_POINT ( 'NONE', #26180 ) ;
#131489=FACE_OUTER_BOUND ( 'NONE', #113945, .T. ) ;
#131490=LINE ( 'NONE', #62671, #120911 ) ;
#131492=EDGE_CURVE ( 'NONE', #97655, #141246, #75414, .T. ) ;
#131493=ORIENTED_EDGE ( 'NONE', *, *, #46296, .F. ) ;
#131494=AXIS2_PLACEMENT_3D ( 'NONE', #3733, #82093, #111839 ) ;
#131495=EDGE_CURVE ( 'NONE', #32915, #135400, #94271, .T. ) ;
#131497=VERTEX_POINT ( 'NONE', #39938 ) ;
#131498=CARTESIAN_POINT ( 'NONE',  ( -48.18398860626899705, 28.73617430169820608, 5.000000000000000000 ) ) ;
#131499=DIRECTION ( 'NONE',  ( -0.7071067811865486830, 0.7071067811865464625, 0.000000000000000000 ) ) ;
#131501=DIRECTION ( 'NONE',  ( -0.7071067811865486830, -0.7071067811865464625, -0.000000000000000000 ) ) ;
#131502=VECTOR ( 'NONE', #116877, 1000.000000000000000 ) ;
#131503=FACE_BOUND ( 'NONE', #68135, .T. ) ;
#131504=EDGE_CURVE ( 'NONE', #37411, #87872, #84155, .T. ) ;
#131505=DIRECTION ( 'NONE',  ( -0.3543493200069162685, -0.000000000000000000, -0.9351131265310288487 ) ) ;
#131506=DIRECTION ( 'NONE',  ( -0.7071067811865487940, 0.7071067811865463515, -0.000000000000000000 ) ) ;
#131507=CARTESIAN_POINT ( 'NONE',  ( -8.671830600776413434, 11.25929247661560240, 4.000000000000000000 ) ) ;
#131509=ORIENTED_EDGE ( 'NONE', *, *, #63356, .F. ) ;
#131510=AXIS2_PLACEMENT_3D ( 'NONE', #71277, #47422, #16122 ) ;
#131511=VECTOR ( 'NONE', #91924, 1000.000000000000000 ) ;
#131516=EDGE_LOOP ( 'NONE', ( #76413, #76901, #111309, #59436 ) ) ;
#131517=CARTESIAN_POINT ( 'NONE',  ( -7.499999999999945821, 15.05218569542901896, 5.000000000000000000 ) ) ;
#131518=VERTEX_POINT ( 'NONE', #17423 ) ;
#131519=LINE ( 'NONE', #117052, #100289 ) ;
#131520=CARTESIAN_POINT ( 'NONE',  ( -1.499999999999990896, -2.173586137069142499, -4.605770156576112662 ) ) ;
#131521=DIRECTION ( 'NONE',  ( 0.7071067811865486830, -0.7071067811865464625, -0.000000000000000000 ) ) ;
#131522=CARTESIAN_POINT ( 'NONE',  ( -13.49999999999990941, 12.05218569542904561, 5.000000000000000000 ) ) ;
#131523=CARTESIAN_POINT ( 'NONE',  ( 2.999999999999985345, 8.587461875839158765, 4.000000000000000000 ) ) ;
#131524=DIRECTION ( 'NONE',  ( -0.7071067811865486830, 0.7071067811865464625, 0.000000000000000000 ) ) ;
#131525=FACE_OUTER_BOUND ( 'NONE', #97851, .T. ) ;
#131526=EDGE_LOOP ( 'NONE', ( #109200, #97171, #43263, #40598 ) ) ;
#131528=ORIENTED_EDGE ( 'NONE', *, *, #66457, .T. ) ;
#131529=DIRECTION ( 'NONE',  ( 0.7071067811865487940, 0.7071067811865463515, 0.000000000000000000 ) ) ;
#131530=CARTESIAN_POINT ( 'NONE',  ( 6.989119713460463679, -22.02621442084248216, 4.990779571109220214 ) ) ;
#131532=VERTEX_POINT ( 'NONE', #116743 ) ;
#131533=ORIENTED_EDGE ( 'NONE', *, *, #38948, .F. ) ;
#131536=EDGE_LOOP ( 'NONE', ( #52738, #60131, #127234, #57230 ) ) ;
#131537=CARTESIAN_POINT ( 'NONE',  ( 72.48921356237309510, -27.52281430457106026, 5.000000000000000000 ) ) ;
#131538=LINE ( 'NONE', #88768, #118729 ) ;
#131542=EDGE_CURVE ( 'NONE', #47759, #130435, #115268, .T. ) ;
#131543=ORIENTED_EDGE ( 'NONE', *, *, #30395, .T. ) ;
#131545=EDGE_CURVE ( 'NONE', #137465, #96120, #139954, .T. ) ;
#131546=VERTEX_POINT ( 'NONE', #49388 ) ;
#131548=DIRECTION ( 'NONE',  ( -0.7071067811865486830, -0.7071067811865464625, 0.000000000000000000 ) ) ;
#131549=VECTOR ( 'NONE', #125292, 1000.000000000000114 ) ;
#131550=DIRECTION ( 'NONE',  ( 0.6830127018922181881, 0.6830127018922202975, -0.2588190451025214056 ) ) ;
#131551=VERTEX_POINT ( 'NONE', #96386 ) ;
#131552=ORIENTED_EDGE ( 'NONE', *, *, #81995, .T. ) ;
#131553=ADVANCED_FACE ( 'NONE', ( #83418 ), #16716, .F. ) ;
#131554=PLANE ( 'NONE',  #45057 ) ;
#131555=CARTESIAN_POINT ( 'NONE',  ( 14.81601139373099585, 28.73617430169776910, 5.000000000000000000 ) ) ;
#131556=VECTOR ( 'NONE', #137305, 1000.000000000000000 ) ;
#131557=CARTESIAN_POINT ( 'NONE',  ( 33.52400138585425537, 22.03583458319438648, 4.979811245910084949 ) ) ;
#131558=ORIENTED_EDGE ( 'NONE', *, *, #113604, .F. ) ;
#131560=VERTEX_POINT ( 'NONE', #105153 ) ;
#131561=VERTEX_POINT ( 'NONE', #71845 ) ;
#131562=EDGE_CURVE ( 'NONE', #36893, #4917, #29713, .T. ) ;
#131563=DIRECTION ( 'NONE',  ( -0.7071067811865486830, -0.7071067811865464625, 0.000000000000000000 ) ) ;
#131564=LINE ( 'NONE', #132306, #125059 ) ;
#131566=DIRECTION ( 'NONE',  ( -0.6830127018922180770, -0.6830127018922204085, -0.2588190451025213501 ) ) ;
#131567=DIRECTION ( 'NONE',  ( 0.7071067811865487940, -0.7071067811865463515, 0.000000000000000000 ) ) ;
#131568=EDGE_CURVE ( 'NONE', #62743, #6620, #126883, .T. ) ;
#131569=DIRECTION ( 'NONE',  ( -0.6830127018922180770, -0.6830127018922204085, -0.2588190451025213501 ) ) ;
#131570=CARTESIAN_POINT ( 'NONE',  ( -24.29974487139158867, -27.71228299555223273, 4.000000000000000000 ) ) ;
#131572=VERTEX_POINT ( 'NONE', #27578 ) ;
#131573=LINE ( 'NONE', #85916, #81397 ) ;
#131574=ORIENTED_EDGE ( 'NONE', *, *, #30389, .T. ) ;
#131575=CARTESIAN_POINT ( 'NONE',  ( 27.48921356237309155, -27.52281430457074762, 5.000000000000000000 ) ) ;
#131577=CARTESIAN_POINT ( 'NONE',  ( 24.48921356237309510, -27.52281430457072631, 5.000000000000000000 ) ) ;
#131578=SPHERICAL_SURFACE ( 'NONE', #129455, 0.5000000000000000000 ) ;
#131580=PLANE ( 'NONE',  #113147 ) ;
#131581=VECTOR ( 'NONE', #255, 1000.000000000000227 ) ;
#131582=LINE ( 'NONE', #7069, #48814 ) ;
#131583=DIRECTION ( 'NONE',  ( -0.000000000000000000, 0.000000000000000000, 1.000000000000000000 ) ) ;
#131584=ORIENTED_EDGE ( 'NONE', *, *, #48950, .F. ) ;
#131585=ORIENTED_EDGE ( 'NONE', *, *, #90309, .F. ) ;
#131587=DIRECTION ( 'NONE',  ( -0.3543493200069162685, -0.000000000000000000, -0.9351131265310288487 ) ) ;
#131588=DIRECTION ( 'NONE',  ( -0.7071067811865486830, -0.7071067811865464625, 0.000000000000000000 ) ) ;
#131589=CARTESIAN_POINT ( 'NONE',  ( 10.17183060077640455, 9.759292476615618384, 4.000000000000000000 ) ) ;
#131590=DIRECTION ( 'NONE',  ( -0.7071067811865487940, 0.7071067811865463515, 0.000000000000000000 ) ) ;
#131592=DIRECTION ( 'NONE',  ( -0.7071067811865486830, -0.7071067811865464625, 0.000000000000000000 ) ) ;
#131593=LINE ( 'NONE', #65670, #120199 ) ;
#131594=PLANE ( 'NONE',  #113620 ) ;
#131595=CARTESIAN_POINT ( 'NONE',  ( 23.29289321881329045, 20.25929247661551358, 5.000000000000000000 ) ) ;
#131597=LINE ( 'NONE', #142483, #30288 ) ;
#131598=EDGE_CURVE ( 'NONE', #127400, #116795, #60252, .T. ) ;
#131599=VERTEX_POINT ( 'NONE', #73264 ) ;
#131600=CARTESIAN_POINT ( 'NONE',  ( -22.26506670282036993, 12.75929247661558286, 18.34774599283961294 ) ) ;
#131602=VERTEX_POINT ( 'NONE', #117427 ) ;
#131603=VECTOR ( 'NONE', #42732, 1000.000000000000000 ) ;
#131605=CARTESIAN_POINT ( 'NONE',  ( 0.000000000000000000, 0.000000000000000000, 5.000000000000000000 ) ) ;
#131606=LINE ( 'NONE', #10509, #37318 ) ;
#131607=AXIS2_PLACEMENT_3D ( 'NONE', #88176, #143256, #54841 ) ;
#131609=DIRECTION ( 'NONE',  ( 0.7071067811865487940, 0.7071067811865463515, -0.000000000000000000 ) ) ;
#131611=DIRECTION ( 'NONE',  ( -0.6830127018922181881, 0.6830127018922202975, -0.2588190451025214056 ) ) ;
#131612=VERTEX_POINT ( 'NONE', #5805 ) ;
#131613=ORIENTED_EDGE ( 'NONE', *, *, #32136, .F. ) ;
#131615=DIRECTION ( 'NONE',  ( -0.7071067811865486830, -0.7071067811865464625, 0.000000000000000000 ) ) ;
#131618=VECTOR ( 'NONE', #26839, 1000.000000000000000 ) ;
#131619=CARTESIAN_POINT ( 'NONE',  ( -28.17183060077627488, -20.24070752338407431, 4.000000000000000000 ) ) ;
#131620=EDGE_CURVE ( 'NONE', #39821, #141489, #18104, .T. ) ;
#131621=LINE ( 'NONE', #112014, #27388 ) ;
#131627=CARTESIAN_POINT ( 'NONE',  ( 30.18398860626900060, 28.73617430169808173, 5.000000000000000000 ) ) ;
#131628=EDGE_CURVE ( 'NONE', #103228, #67897, #50081, .T. ) ;
#131629=FACE_OUTER_BOUND ( 'NONE', #133175, .T. ) ;
#131630=DIRECTION ( 'NONE',  ( -0.7071067811865486830, -0.7071067811865464625, -0.000000000000000000 ) ) ;
#131632=VERTEX_POINT ( 'NONE', #51508 ) ;
#131633=FACE_OUTER_BOUND ( 'NONE', #82974, .T. ) ;
#131634=ORIENTED_EDGE ( 'NONE', *, *, #22351, .T. ) ;
#131635=VECTOR ( 'NONE', #61560, 1000.000000000000227 ) ;
#131636=EDGE_CURVE ( 'NONE', #57761, #73971, #7235, .T. ) ;
#131639=VERTEX_POINT ( 'NONE', #119570 ) ;
#131640=LINE ( 'NONE', #76560, #2565 ) ;
#131641=VECTOR ( 'NONE', #88992, 1000.000000000000000 ) ;
#131642=CARTESIAN_POINT ( 'NONE',  ( -34.92500000000001137, -0.2815095627957688307, 4.759050581649336920 ) ) ;
#131643=CARTESIAN_POINT ( 'NONE',  ( -57.48921356237308800, -27.52281430457095368, 5.000000000000000000 ) ) ;
#131644=VECTOR ( 'NONE', #25988, 1000.000000000000000 ) ;
#131646=EDGE_CURVE ( 'NONE', #107864, #112008, #77553, .T. ) ;
#131647=CARTESIAN_POINT ( 'NONE',  ( -0.4892135623730947680, -27.52281430457055578, 5.000000000000000000 ) ) ;
#131648=CARTESIAN_POINT ( 'NONE',  ( 29.20710678118634718, -20.24070752338407075, 5.000000000000000000 ) ) ;
#131649=ORIENTED_EDGE ( 'NONE', *, *, #82503, .T. ) ;
#131650=FACE_OUTER_BOUND ( 'NONE', #126841, .T. ) ;
#131652=CARTESIAN_POINT ( 'NONE',  ( 0.000000000000000000, 0.000000000000000000, 5.000000000000000000 ) ) ;
#131653=VECTOR ( 'NONE', #83285, 1000.000000000000000 ) ;
#131654=LINE ( 'NONE', #133788, #101677 ) ;
#131655=ORIENTED_EDGE ( 'NONE', *, *, #126955, .T. ) ;
#131656=ORIENTED_EDGE ( 'NONE', *, *, #6913, .F. ) ;
#131658=EDGE_LOOP ( 'NONE', ( #17371, #112044, #41399, #85277 ) ) ;
#131659=DIRECTION ( 'NONE',  ( 0.6830127018922181881, 0.6830127018922202975, -0.2588190451025214056 ) ) ;
#131660=DIRECTION ( 'NONE',  ( 1.000000000000000000, 0.000000000000000000, 0.000000000000000000 ) ) ;
#131661=LINE ( 'NONE', #96836, #75854 ) ;
#131663=ORIENTED_EDGE ( 'NONE', *, *, #138401, .F. ) ;
#131664=VERTEX_POINT ( 'NONE', #88423 ) ;
#131665=VECTOR ( 'NONE', #51881, 999.9999999999998863 ) ;
#131666=CARTESIAN_POINT ( 'NONE',  ( 9.005480084712511157, 28.92564299267931816, 4.000000000000000000 ) ) ;
#131667=LINE ( 'NONE', #107740, #4974 ) ;
#131668=VECTOR ( 'NONE', #56754, 1000.000000000000000 ) ;
#131669=ORIENTED_EDGE ( 'NONE', *, *, #6168, .F. ) ;
#131670=EDGE_CURVE ( 'NONE', #28630, #46262, #20266, .T. ) ;
#131671=LINE ( 'NONE', #11269, #2644 ) ;
#131672=CARTESIAN_POINT ( 'NONE',  ( -3.299744871391591339, -27.71228299555208352, 4.000000000000000000 ) ) ;
#131673=DIRECTION ( 'NONE',  ( -0.3543493200069163240, -0.000000000000000000, 0.9351131265310288487 ) ) ;
#131676=FACE_BOUND ( 'NONE', #48763, .T. ) ;
#131679=CARTESIAN_POINT ( 'NONE',  ( 20.67183060077633883, 20.25929247661551713, 4.000000000000000000 ) ) ;
#131680=CARTESIAN_POINT ( 'NONE',  ( 0.000000000000000000, 0.000000000000000000, 5.000000000000000000 ) ) ;
#131682=PLANE ( 'NONE',  #23378 ) ;
#131683=VERTEX_POINT ( 'NONE', #66663 ) ;
#131684=ORIENTED_EDGE ( 'NONE', *, *, #128938, .F. ) ;
#131686=ORIENTED_EDGE ( 'NONE', *, *, #142147, .T. ) ;
#131688=CARTESIAN_POINT ( 'NONE',  ( -16.00193056682086379, -22.22500000000000142, 4.500000000000000888 ) ) ;
#131689=ADVANCED_FACE ( 'NONE', ( #110131 ), #53644, .T. ) ;
#131690=CARTESIAN_POINT ( 'NONE',  ( 21.00548008471250938, 28.92564299267923644, 4.000000000000000000 ) ) ;
#131691=CARTESIAN_POINT ( 'NONE',  ( -51.18398860626899705, 28.73617430169823095, 5.000000000000000000 ) ) ;
#131692=ORIENTED_EDGE ( 'NONE', *, *, #9062, .F. ) ;
#131693=DIRECTION ( 'NONE',  ( 0.3543493200069162685, -0.000000000000000000, -0.9351131265310288487 ) ) ;
#131695=DIRECTION ( 'NONE',  ( 1.000000000000000000, 0.000000000000000000, 0.000000000000000000 ) ) ;
#131696=LINE ( 'NONE', #86772, #126786 ) ;
#131698=VECTOR ( 'NONE', #79503, 1000.000000000000000 ) ;
#131699=AXIS2_PLACEMENT_3D ( 'NONE', #64906, #40997, #118542 ) ;
#131700=CARTESIAN_POINT ( 'NONE',  ( 31.49999999999977263, 19.08746187583906462, 4.000000000000000000 ) ) ;
#131701=VECTOR ( 'NONE', #125444, 1000.000000000000227 ) ;
#131702=ORIENTED_EDGE ( 'NONE', *, *, #28622, .F. ) ;
#131703=CARTESIAN_POINT ( 'NONE',  ( -8.994519915287490619, 28.92564299267944250, 4.000000000000000000 ) ) ;
#131704=FACE_OUTER_BOUND ( 'NONE', #108034, .T. ) ;
#131705=ORIENTED_EDGE ( 'NONE', *, *, #75562, .T. ) ;
#131706=ORIENTED_EDGE ( 'NONE', *, *, #131542, .T. ) ;
#131707=VERTEX_POINT ( 'NONE', #86972 ) ;
#131711=VECTOR ( 'NONE', #136554, 1000.000000000000000 ) ;
#131712=CARTESIAN_POINT ( 'NONE',  ( -23.99999999999983302, 13.55218569542903317, 5.000000000000000000 ) ) ;
#131713=ADVANCED_FACE ( 'NONE', ( #86277 ), #131192, .F. ) ;
#131716=DIRECTION ( 'NONE',  ( -0.3543493200069162685, -0.000000000000000000, -0.9351131265310288487 ) ) ;
#131717=ADVANCED_FACE ( 'NONE', ( #85519, #110828 ), #129758, .F. ) ;
#131718=DIRECTION ( 'NONE',  ( -0.7071067811865487940, 0.7071067811865463515, -0.000000000000000000 ) ) ;
#131720=FACE_OUTER_BOUND ( 'NONE', #76522, .T. ) ;
#131721=AXIS2_PLACEMENT_3D ( 'NONE', #113924, #125532, #126235 ) ;
#131722=FACE_OUTER_BOUND ( 'NONE', #61290, .T. ) ;
#131723=EDGE_CURVE ( 'NONE', #46898, #67112, #130499, .T. ) ;
#131724=EDGE_CURVE ( 'NONE', #91593, #143231, #76102, .T. ) ;
#131726=DIRECTION ( 'NONE',  ( -0.3543493200069162685, -0.000000000000000000, -0.9351131265310288487 ) ) ;
#131727=CARTESIAN_POINT ( 'NONE',  ( 14.20710678118644132, -11.24070752338417023, 5.000000000000000000 ) ) ;
#131729=AXIS2_PLACEMENT_3D ( 'NONE', #1070, #122874, #14094 ) ;
#131730=LINE ( 'NONE', #140446, #106210 ) ;
#131732=ORIENTED_EDGE ( 'NONE', *, *, #135573, .T. ) ;
#131733=ORIENTED_EDGE ( 'NONE', *, *, #882, .T. ) ;
#131735=ORIENTED_EDGE ( 'NONE', *, *, #112036, .T. ) ;
#131736=VECTOR ( 'NONE', #26448, 1000.000000000000000 ) ;
#131739=DIRECTION ( 'NONE',  ( -0.7071067811865486830, 0.7071067811865464625, 0.000000000000000000 ) ) ;
#131740=AXIS2_PLACEMENT_3D ( 'NONE', #105530, #114281, #70807 ) ;
#131741=ADVANCED_FACE ( 'NONE', ( #109434 ), #43471, .F. ) ;
#131743=ADVANCED_FACE ( 'NONE', ( #26009 ), #57236, .F. ) ;
#131744=ORIENTED_EDGE ( 'NONE', *, *, #8875, .F. ) ;
#131745=LINE ( 'NONE', #9188, #39575 ) ;
#131746=ORIENTED_EDGE ( 'NONE', *, *, #31755, .T. ) ;
#131747=VECTOR ( 'NONE', #45691, 1000.000000000000000 ) ;
#131748=ADVANCED_FACE ( 'NONE', ( #663 ), #36863, .T. ) ;
#131750=FACE_OUTER_BOUND ( 'NONE', #82046, .T. ) ;
#131752=PLANE ( 'NONE',  #138641 ) ;
#131754=ORIENTED_EDGE ( 'NONE', *, *, #96192, .F. ) ;
#131755=VERTEX_POINT ( 'NONE', #111580 ) ;
#131756=VERTEX_POINT ( 'NONE', #47791 ) ;
#131759=EDGE_CURVE ( 'NONE', #56470, #26097, #78986, .T. ) ;
#131760=VECTOR ( 'NONE', #70635, 1000.000000000000000 ) ;
#131761=DIRECTION ( 'NONE',  ( -0.000000000000000000, -0.3543493200069152693, 0.9351131265310292928 ) ) ;
#131762=PLANE ( 'NONE',  #140892 ) ;
#131763=CARTESIAN_POINT ( 'NONE',  ( -48.29974487139158867, -27.71228299555239971, 4.000000000000000000 ) ) ;
#131765=DIRECTION ( 'NONE',  ( 0.3543493200069162685, -0.000000000000000000, -0.9351131265310288487 ) ) ;
#131766=CARTESIAN_POINT ( 'NONE',  ( 19.05000000000000071, 3.174999999999997158, 4.000000000000000000 ) ) ;
#131767=ORIENTED_EDGE ( 'NONE', *, *, #95558, .F. ) ;
#131768=PLANE ( 'NONE',  #90533 ) ;
#131769=EDGE_CURVE ( 'NONE', #42960, #116177, #23867, .T. ) ;
#131770=ORIENTED_EDGE ( 'NONE', *, *, #26089, .F. ) ;
#131772=EDGE_LOOP ( 'NONE', ( #51539, #87295, #67522, #3260 ) ) ;
#131774=DIRECTION ( 'NONE',  ( -0.6830127018922181881, 0.6830127018922202975, -0.2588190451025214056 ) ) ;
#131775=VERTEX_POINT ( 'NONE', #114429 ) ;
#131776=CARTESIAN_POINT ( 'NONE',  ( -9.792893218813391698, -20.24070752338407431, 5.000000000000000000 ) ) ;
#131777=EDGE_CURVE ( 'NONE', #113899, #76633, #34042, .T. ) ;
#131778=ORIENTED_EDGE ( 'NONE', *, *, #38243, .T. ) ;
#131779=DIRECTION ( 'NONE',  ( -0.6830127018922180770, 0.6830127018922202975, -0.2588190451025213501 ) ) ;
#131780=ORIENTED_EDGE ( 'NONE', *, *, #73052, .T. ) ;
#131781=DIRECTION ( 'NONE',  ( -0.6830127018922180770, -0.6830127018922204085, -0.2588190451025213501 ) ) ;
#131782=EDGE_LOOP ( 'NONE', ( #106696, #40294, #103207, #37088 ) ) ;
#131783=CARTESIAN_POINT ( 'NONE',  ( 59.99451991528749772, 28.92564299267980132, 4.000000000000000000 ) ) ;
#131784=ADVANCED_FACE ( 'NONE', ( #36178 ), #125318, .F. ) ;
#131788=CARTESIAN_POINT ( 'NONE',  ( 71.99451991528749772, 28.92564299267988304, 4.000000000000000000 ) ) ;
#131790=LINE ( 'NONE', #32479, #83209 ) ;
#131794=FACE_OUTER_BOUND ( 'NONE', #86221, .T. ) ;
#131795=VERTEX_POINT ( 'NONE', #59375 ) ;
#131796=VERTEX_POINT ( 'NONE', #113722 ) ;
#131797=DIRECTION ( 'NONE',  ( 1.000000000000000000, 0.000000000000000000, 0.000000000000000000 ) ) ;
#131798=ORIENTED_EDGE ( 'NONE', *, *, #5153, .T. ) ;
#131799=EDGE_CURVE ( 'NONE', #70593, #20021, #44954, .T. ) ;
#131803=ORIENTED_EDGE ( 'NONE', *, *, #1762, .F. ) ;
#131804=VECTOR ( 'NONE', #74873, 1000.000000000000000 ) ;
#131805=VECTOR ( 'NONE', #125453, 1000.000000000000227 ) ;
#131806=AXIS2_PLACEMENT_3D ( 'NONE', #56968, #134512, #102600 ) ;
#131808=CARTESIAN_POINT ( 'NONE',  ( 8.510786437626906675, -27.52281430457049183, 5.000000000000000000 ) ) ;
#131809=VECTOR ( 'NONE', #128139, 999.9999999999998863 ) ;
#131810=DIRECTION ( 'NONE',  ( -0.000000000000000000, 0.3543493200069153248, 0.9351131265310292928 ) ) ;
#131811=CARTESIAN_POINT ( 'NONE',  ( 0.1839886062690032631, 28.73617430169787568, 5.000000000000000000 ) ) ;
#131812=EDGE_CURVE ( 'NONE', #137018, #100179, #102151, .T. ) ;
#131814=DIRECTION ( 'NONE',  ( 0.7071067811865487940, -0.7071067811865463515, 0.000000000000000000 ) ) ;
#131815=ORIENTED_EDGE ( 'NONE', *, *, #140213, .F. ) ;
#131816=DIRECTION ( 'NONE',  ( -0.000000000000000000, -0.3543493200069152693, 0.9351131265310292928 ) ) ;
#131818=PLANE ( 'NONE',  #71101 ) ;
#131819=VECTOR ( 'NONE', #41352, 1000.000000000000000 ) ;
#131820=CARTESIAN_POINT ( 'NONE',  ( 34.42499999999998295, -4.458600742197917910, 5.000000000000000000 ) ) ;
#131821=EDGE_LOOP ( 'NONE', ( #137537, #37835, #87645, #128840 ) ) ;
#131825=ORIENTED_EDGE ( 'NONE', *, *, #27747, .F. ) ;
#131826=EDGE_CURVE ( 'NONE', #23670, #489, #112310, .T. ) ;
#131828=VECTOR ( 'NONE', #117293, 1000.000000000000227 ) ;
#131829=VECTOR ( 'NONE', #108951, 999.9999999999998863 ) ;
#131830=CARTESIAN_POINT ( 'NONE',  ( -7.499999999999944045, 3.052185695429140200, 5.000000000000000000 ) ) ;
#131831=ORIENTED_EDGE ( 'NONE', *, *, #100741, .T. ) ;
#131836=VERTEX_POINT ( 'NONE', #12258 ) ;
#131837=EDGE_CURVE ( 'NONE', #66659, #130638, #124599, .T. ) ;
#131838=CARTESIAN_POINT ( 'NONE',  ( 54.18398860626899705, 28.73617430169825226, 5.000000000000000000 ) ) ;
#131839=LINE ( 'NONE', #20184, #130218 ) ;
#131841=VECTOR ( 'NONE', #37825, 1000.000000000000227 ) ;
#131842=ORIENTED_EDGE ( 'NONE', *, *, #132137, .F. ) ;
#131843=EDGE_LOOP ( 'NONE', ( #131754, #8915, #61929, #60204 ) ) ;
#131844=EDGE_CURVE ( 'NONE', #73748, #36255, #23106, .T. ) ;
#131845=ORIENTED_EDGE ( 'NONE', *, *, #29236, .F. ) ;
#131846=CARTESIAN_POINT ( 'NONE',  ( 28.49999999999980105, 18.43112307739199451, 4.000000000000000000 ) ) ;
#131847=VECTOR ( 'NONE', #78342, 1000.000000000000227 ) ;
#131848=EDGE_CURVE ( 'NONE', #131518, #50635, #89133, .T. ) ;
#131849=CARTESIAN_POINT ( 'NONE',  ( -26.99999999999980815, -21.41253812416053748, 4.000000000000000000 ) ) ;
#131850=CARTESIAN_POINT ( 'NONE',  ( 0.4892135623730947680, -27.52281430457055578, 5.000000000000000000 ) ) ;
#131852=AXIS2_PLACEMENT_3D ( 'NONE', #111762, #79890, #54544 ) ;
#131854=PLANE ( 'NONE',  #25633 ) ;
#131856=ORIENTED_EDGE ( 'NONE', *, *, #102114, .F. ) ;
#131857=EDGE_CURVE ( 'NONE', #69033, #96928, #79724, .T. ) ;
#131858=VERTEX_POINT ( 'NONE', #135495 ) ;
#131859=DIRECTION ( 'NONE',  ( -0.7071067811865486830, -0.7071067811865464625, 0.000000000000000000 ) ) ;
#131860=ORIENTED_EDGE ( 'NONE', *, *, #138090, .F. ) ;
#131861=VERTEX_POINT ( 'NONE', #25274 ) ;
#131862=VECTOR ( 'NONE', #123942, 1000.000000000000000 ) ;
#131863=EDGE_CURVE ( 'NONE', #49923, #134381, #78258, .T. ) ;
#131864=DIRECTION ( 'NONE',  ( -0.7071067811865487940, 0.7071067811865463515, -0.000000000000000000 ) ) ;
#131865=EDGE_LOOP ( 'NONE', ( #112648, #60378, #73721, #3792 ) ) ;
#131866=LINE ( 'NONE', #8592, #25084 ) ;
#131868=DIRECTION ( 'NONE',  ( -0.7071067811865486830, -0.7071067811865464625, -0.000000000000000000 ) ) ;
#131869=LINE ( 'NONE', #45600, #11304 ) ;
#131870=DIRECTION ( 'NONE',  ( -0.7071067811865487940, 0.7071067811865463515, -0.000000000000000000 ) ) ;
#131871=ORIENTED_EDGE ( 'NONE', *, *, #131826, .F. ) ;
#131873=ORIENTED_EDGE ( 'NONE', *, *, #10218, .F. ) ;
#131874=LINE ( 'NONE', #130458, #20228 ) ;
#131875=EDGE_LOOP ( 'NONE', ( #21730, #31627, #115418, #74461 ) ) ;
#131879=DIRECTION ( 'NONE',  ( 0.7071067811865487940, 0.7071067811865463515, -0.000000000000000000 ) ) ;
#131880=ORIENTED_EDGE ( 'NONE', *, *, #66124, .T. ) ;
#131881=ORIENTED_EDGE ( 'NONE', *, *, #104399, .T. ) ;
#131882=VERTEX_POINT ( 'NONE', #14412 ) ;
#131883=CARTESIAN_POINT ( 'NONE',  ( -57.29974487139158157, -27.71228299555246011, 4.000000000000000000 ) ) ;
#131885=PLANE ( 'NONE',  #87766 ) ;
#131886=CARTESIAN_POINT ( 'NONE',  ( -2.816011393730999401, 28.73617430169785436, 5.000000000000000000 ) ) ;
#131888=DIRECTION ( 'NONE',  ( -0.000000000000000000, 0.3543493200069153248, 0.9351131265310292928 ) ) ;
#131889=EDGE_CURVE ( 'NONE', #71084, #83494, #89819, .T. ) ;
#131891=CARTESIAN_POINT ( 'NONE',  ( -26.29289321881326913, 14.25929247661557220, 5.000000000000000000 ) ) ;
#131892=CARTESIAN_POINT ( 'NONE',  ( 24.48921356237309510, -27.52281430457072631, 5.000000000000000000 ) ) ;
#131893=CARTESIAN_POINT ( 'NONE',  ( -34.49999999999975842, 22.01701374228152730, 2.453858888625711110 ) ) ;
#131895=EDGE_CURVE ( 'NONE', #46307, #141426, #52562, .T. ) ;
#131897=CARTESIAN_POINT ( 'NONE',  ( 24.48921356237309510, -27.52281430457072631, 5.000000000000000000 ) ) ;
#131898=CARTESIAN_POINT ( 'NONE',  ( 4.499999999999968914, 9.052185695429077583, 5.000000000000000000 ) ) ;
#131901=AXIS2_PLACEMENT_3D ( 'NONE', #26643, #38951, #93328 ) ;
#131902=ORIENTED_EDGE ( 'NONE', *, *, #89445, .T. ) ;
#131903=CARTESIAN_POINT ( 'NONE',  ( -8.292893218813384593, -15.74070752338412049, 5.000000000000000000 ) ) ;
#131904=VECTOR ( 'NONE', #50777, 1000.000000000000000 ) ;
#131905=ORIENTED_EDGE ( 'NONE', *, *, #61781, .T. ) ;
#131906=VECTOR ( 'NONE', #97383, 999.9999999999998863 ) ;
#131907=EDGE_CURVE ( 'NONE', #57945, #63482, #118533, .T. ) ;
#131909=VERTEX_POINT ( 'NONE', #48463 ) ;
#131910=CARTESIAN_POINT ( 'NONE',  ( 42.18398860626899705, 28.73617430169816700, 5.000000000000000000 ) ) ;
#131912=ADVANCED_FACE ( 'NONE', ( #92664 ), #49207, .F. ) ;
#131913=EDGE_CURVE ( 'NONE', #38574, #18661, #20639, .T. ) ;
#131914=DIRECTION ( 'NONE',  ( 0.3543493200069162685, -0.000000000000000000, -0.9351131265310288487 ) ) ;
#131915=ORIENTED_EDGE ( 'NONE', *, *, #21447, .T. ) ;
#131916=FACE_OUTER_BOUND ( 'NONE', #67944, .T. ) ;
#131920=PLANE ( 'NONE',  #35827 ) ;
#131921=EDGE_CURVE ( 'NONE', #7595, #59056, #130874, .T. ) ;
#131923=VECTOR ( 'NONE', #102876, 1000.000000000000000 ) ;
#131924=ORIENTED_EDGE ( 'NONE', *, *, #84623, .T. ) ;
#131926=EDGE_CURVE ( 'NONE', #134787, #68809, #108334, .T. ) ;
#131928=CARTESIAN_POINT ( 'NONE',  ( -5.994519915287488843, 28.92564299267942118, 4.000000000000000000 ) ) ;
#131929=CARTESIAN_POINT ( 'NONE',  ( 0.000000000000000000, 0.000000000000000000, 5.000000000000000000 ) ) ;
#131932=EDGE_LOOP ( 'NONE', ( #73632, #67981, #42830, #84633 ) ) ;
#131933=PLANE ( 'NONE',  #35759 ) ;
#131934=VECTOR ( 'NONE', #121946, 1000.000000000000000 ) ;
#131935=FACE_OUTER_BOUND ( 'NONE', #72083, .T. ) ;
#131938=EDGE_CURVE ( 'NONE', #116539, #97084, #75072, .T. ) ;
#131939=CARTESIAN_POINT ( 'NONE',  ( -5.999999999999954703, -0.4125381241607533611, 4.000000000000000000 ) ) ;
#131940=CARTESIAN_POINT ( 'NONE',  ( 23.67183060077630685, 11.25929247661559884, 4.000000000000000000 ) ) ;
#131941=ORIENTED_EDGE ( 'NONE', *, *, #24988, .F. ) ;
#131942=DIRECTION ( 'NONE',  ( 0.7071067811865487940, 0.7071067811865463515, 0.000000000000000000 ) ) ;
#131945=CARTESIAN_POINT ( 'NONE',  ( -75.18398860626899705, 28.73617430169839793, 5.000000000000000000 ) ) ;
#131946=ORIENTED_EDGE ( 'NONE', *, *, #28726, .T. ) ;
#131948=ADVANCED_FACE ( 'NONE', ( #9008 ), #29374, .F. ) ;
#131949=VECTOR ( 'NONE', #143223, 1000.000000000000000 ) ;
#131950=CARTESIAN_POINT ( 'NONE',  ( -15.79289321881334551, 18.75929247661552424, 5.000000000000000000 ) ) ;
#131952=ORIENTED_EDGE ( 'NONE', *, *, #92112, .F. ) ;
#131953=VECTOR ( 'NONE', #30322, 1000.000000000000227 ) ;
#131954=CARTESIAN_POINT ( 'NONE',  ( -11.99451991528749417, 28.92564299267946382, 4.000000000000000000 ) ) ;
#131955=VERTEX_POINT ( 'NONE', #60074 ) ;
#131956=ORIENTED_EDGE ( 'NONE', *, *, #101594, .T. ) ;
#131957=AXIS2_PLACEMENT_3D ( 'NONE', #27553, #60974, #105133 ) ;
#131958=DIRECTION ( 'NONE',  ( 1.000000000000000000, 0.000000000000000000, 0.000000000000000000 ) ) ;
#131960=CARTESIAN_POINT ( 'NONE',  ( -9.489213562373095101, -27.52281430457062328, 5.000000000000000000 ) ) ;
#131961=EDGE_LOOP ( 'NONE', ( #42913, #133050, #27516, #137885 ) ) ;
#131962=DIRECTION ( 'NONE',  ( -0.7071067811865486830, -0.7071067811865464625, 0.000000000000000000 ) ) ;
#131964=EDGE_CURVE ( 'NONE', #118228, #76385, #96057, .T. ) ;
#131965=PLANE ( 'NONE',  #138755 ) ;
#131966=CARTESIAN_POINT ( 'NONE',  ( 45.29974487139158867, -27.71228299555237840, 4.000000000000000000 ) ) ;
#131968=LINE ( 'NONE', #42822, #130096 ) ;
#131969=CARTESIAN_POINT ( 'NONE',  ( -13.49999999999991118, -4.796895815301030375, -3.611700055028712164 ) ) ;
#131971=LINE ( 'NONE', #110179, #103636 ) ;
#131972=VECTOR ( 'NONE', #17639, 1000.000000000000000 ) ;
#131973=LINE ( 'NONE', #76153, #102401 ) ;
#131974=DIRECTION ( 'NONE',  ( -0.7071067811865487940, 0.7071067811865463515, 0.000000000000000000 ) ) ;
#131975=EDGE_CURVE ( 'NONE', #40996, #100682, #85910, .T. ) ;
#131976=DIRECTION ( 'NONE',  ( 1.000000000000000000, 0.000000000000000000, 0.000000000000000000 ) ) ;
#131978=ORIENTED_EDGE ( 'NONE', *, *, #11052, .F. ) ;
#131981=ORIENTED_EDGE ( 'NONE', *, *, #133188, .F. ) ;
#131982=ORIENTED_EDGE ( 'NONE', *, *, #33590, .T. ) ;
#131983=EDGE_LOOP ( 'NONE', ( #84542, #77911, #84437, #47012 ) ) ;
#131984=PLANE ( 'NONE',  #105762 ) ;
#131987=VERTEX_POINT ( 'NONE', #63487 ) ;
#131988=CARTESIAN_POINT ( 'NONE',  ( -34.49999999999975131, 12.43112307739205846, 4.000000000000000000 ) ) ;
#131990=DIRECTION ( 'NONE',  ( 1.000000000000000000, 0.000000000000000000, 0.000000000000000000 ) ) ;
#131991=FACE_OUTER_BOUND ( 'NONE', #133612, .T. ) ;
#131992=ORIENTED_EDGE ( 'NONE', *, *, #53213, .T. ) ;
#131994=PLANE ( 'NONE',  #121438 ) ;
#131995=LINE ( 'NONE', #55143, #28212 ) ;
#131996=LINE ( 'NONE', #76918, #5847 ) ;
#131998=CARTESIAN_POINT ( 'NONE',  ( 39.48921356237310221, -27.52281430457082934, 5.000000000000000000 ) ) ;
#131999=LINE ( 'NONE', #31957, #54647 ) ;
#132001=CARTESIAN_POINT ( 'NONE',  ( 0.000000000000000000, 16.93112307739200872, 4.000000000000000000 ) ) ;
#132002=ORIENTED_EDGE ( 'NONE', *, *, #4612, .F. ) ;
#132005=ORIENTED_EDGE ( 'NONE', *, *, #108460, .T. ) ;
#132006=DIRECTION ( 'NONE',  ( -0.000000000000000000, 0.000000000000000000, 1.000000000000000000 ) ) ;
#132007=EDGE_CURVE ( 'NONE', #94828, #56865, #106941, .T. ) ;
#132008=CARTESIAN_POINT ( 'NONE',  ( -26.20710678118636139, 12.75929247661559351, 5.000000000000000000 ) ) ;
#132009=LINE ( 'NONE', #111677, #108182 ) ;
#132014=ORIENTED_EDGE ( 'NONE', *, *, #46410, .T. ) ;
#132015=ORIENTED_EDGE ( 'NONE', *, *, #15049, .T. ) ;
#132017=VECTOR ( 'NONE', #77898, 999.9999999999998863 ) ;
#132018=AXIS2_PLACEMENT_3D ( 'NONE', #113017, #58718, #24589 ) ;
#132021=AXIS2_PLACEMENT_3D ( 'NONE', #43616, #63962, #20420 ) ;
#132022=VERTEX_POINT ( 'NONE', #26711 ) ;
#132023=ORIENTED_EDGE ( 'NONE', *, *, #34063, .F. ) ;
#132025=EDGE_CURVE ( 'NONE', #56807, #80300, #46677, .T. ) ;
#132026=ORIENTED_EDGE ( 'NONE', *, *, #25023, .F. ) ;
#132027=CARTESIAN_POINT ( 'NONE',  ( 15.48921356237309510, -27.52281430457066236, 5.000000000000000000 ) ) ;
#132028=CARTESIAN_POINT ( 'NONE',  ( 29.90156419391745857, 11.25929247661560240, 10.79108189686413866 ) ) ;
#132029=LINE ( 'NONE', #99353, #110850 ) ;
#132030=VECTOR ( 'NONE', #73329, 1000.000000000000000 ) ;
#132031=EDGE_CURVE ( 'NONE', #55786, #42348, #85181, .T. ) ;
#132034=ORIENTED_EDGE ( 'NONE', *, *, #87918, .T. ) ;
#132035=EDGE_CURVE ( 'NONE', #45162, #22876, #137633, .T. ) ;
#132036=LINE ( 'NONE', #32727, #115013 ) ;
#132037=ORIENTED_EDGE ( 'NONE', *, *, #135406, .T. ) ;
#132038=ORIENTED_EDGE ( 'NONE', *, *, #120399, .F. ) ;
#132039=VECTOR ( 'NONE', #139811, 1000.000000000000000 ) ;
#132040=ORIENTED_EDGE ( 'NONE', *, *, #109631, .F. ) ;
#132041=EDGE_CURVE ( 'NONE', #53146, #24456, #82526, .T. ) ;
#132042=VECTOR ( 'NONE', #131337, 1000.000000000000000 ) ;
#132043=DIRECTION ( 'NONE',  ( -0.7071067811865486830, -0.7071067811865464625, 0.000000000000000000 ) ) ;
#132044=ORIENTED_EDGE ( 'NONE', *, *, #20383, .F. ) ;
#132045=DIRECTION ( 'NONE',  ( 0.7071067811865487940, 0.7071067811865463515, -0.000000000000000000 ) ) ;
#132046=VECTOR ( 'NONE', #96102, 1000.000000000000000 ) ;
#132047=FACE_OUTER_BOUND ( 'NONE', #17064, .T. ) ;
#132049=ADVANCED_FACE ( 'NONE', ( #98912 ), #33003, .F. ) ;
#132050=VECTOR ( 'NONE', #76172, 1000.000000000000000 ) ;
#132051=CARTESIAN_POINT ( 'NONE',  ( -6.489213562373093325, -27.52281430457059841, 5.000000000000000000 ) ) ;
#132052=FACE_BOUND ( 'NONE', #86244, .T. ) ;
#132053=VERTEX_POINT ( 'NONE', #22066 ) ;
#132054=LINE ( 'NONE', #55926, #75820 ) ;
#132055=CARTESIAN_POINT ( 'NONE',  ( 11.29289321881338104, -18.74070752338409562, 5.000000000000000000 ) ) ;
#132056=CARTESIAN_POINT ( 'NONE',  ( 0.000000000000000000, 0.000000000000000000, 5.000000000000000000 ) ) ;
#132057=ORIENTED_EDGE ( 'NONE', *, *, #58584, .T. ) ;
#132059=ORIENTED_EDGE ( 'NONE', *, *, #123572, .F. ) ;
#132060=EDGE_CURVE ( 'NONE', #85002, #100524, #65639, .T. ) ;
#132063=CARTESIAN_POINT ( 'NONE',  ( 19.82816939922339827, -14.24070752338414003, 4.000000000000000000 ) ) ;
#132064=ORIENTED_EDGE ( 'NONE', *, *, #135614, .F. ) ;
#132066=ORIENTED_EDGE ( 'NONE', *, *, #32747, .T. ) ;
#132068=CARTESIAN_POINT ( 'NONE',  ( 30.48921356237309510, -27.52281430457076894, 5.000000000000000000 ) ) ;
#132069=LINE ( 'NONE', #43607, #31101 ) ;
#132072=ORIENTED_EDGE ( 'NONE', *, *, #11583, .F. ) ;
#132073=CARTESIAN_POINT ( 'NONE',  ( 7.499999999999949374, 16.77039438581780217, 0.4657186855307575701 ) ) ;
#132074=VECTOR ( 'NONE', #32680, 1000.000000000000000 ) ;
#132075=LINE ( 'NONE', #101550, #13425 ) ;
#132077=ADVANCED_FACE ( 'NONE', ( #11163 ), #134434, .F. ) ;
#132079=CARTESIAN_POINT ( 'NONE',  ( -34.92500000000001137, -21.72500000000000142, 0.4999999999999995559 ) ) ;
#132080=LINE ( 'NONE', #75548, #92257 ) ;
#132082=CARTESIAN_POINT ( 'NONE',  ( -48.29974487139158867, -27.71228299555239971, 4.000000000000000000 ) ) ;
#132084=VERTEX_POINT ( 'NONE', #111969 ) ;
#132085=VECTOR ( 'NONE', #31878, 1000.000000000000000 ) ;
#132088=FACE_OUTER_BOUND ( 'NONE', #118059, .T. ) ;
#132089=ORIENTED_EDGE ( 'NONE', *, *, #108438, .T. ) ;
#132090=ADVANCED_FACE ( 'NONE', ( #55440 ), #34393, .F. ) ;
#132091=ORIENTED_EDGE ( 'NONE', *, *, #88206, .F. ) ;
#132093=FACE_OUTER_BOUND ( 'NONE', #18466, .T. ) ;
#132094=EDGE_CURVE ( 'NONE', #98043, #71394, #143146, .T. ) ;
#132095=LINE ( 'NONE', #77707, #76447 ) ;
#132096=ORIENTED_EDGE ( 'NONE', *, *, #127962, .T. ) ;
#132097=DIRECTION ( 'NONE',  ( 0.6830127018922180770, -0.6830127018922204085, -0.2588190451025213501 ) ) ;
#132098=VECTOR ( 'NONE', #3886, 1000.000000000000000 ) ;
#132099=DIRECTION ( 'NONE',  ( -0.7071067811865486830, -0.7071067811865464625, -0.000000000000000000 ) ) ;
#132101=LINE ( 'NONE', #35665, #55386 ) ;
#132104=ADVANCED_FACE ( 'NONE', ( #133020 ), #45303, .T. ) ;
#132105=DIRECTION ( 'NONE',  ( -0.6830127018922181881, 0.6830127018922202975, -0.2588190451025214056 ) ) ;
#132106=DIRECTION ( 'NONE',  ( 1.000000000000000000, 0.000000000000000000, 0.000000000000000000 ) ) ;
#132107=DIRECTION ( 'NONE',  ( -0.000000000000000000, -0.000000000000000000, 1.000000000000000000 ) ) ;
#132108=ORIENTED_EDGE ( 'NONE', *, *, #101129, .T. ) ;
#132109=PLANE ( 'NONE',  #18435 ) ;
#132110=ORIENTED_EDGE ( 'NONE', *, *, #119927, .T. ) ;
#132111=VECTOR ( 'NONE', #69497, 999.9999999999998863 ) ;
#132112=ADVANCED_FACE ( 'NONE', ( #122828 ), #43846, .F. ) ;
#132113=FACE_OUTER_BOUND ( 'NONE', #133968, .T. ) ;
#132114=DIRECTION ( 'NONE',  ( -0.7071067811865486830, -0.7071067811865464625, 0.000000000000000000 ) ) ;
#132115=ORIENTED_EDGE ( 'NONE', *, *, #42786, .T. ) ;
#132116=VECTOR ( 'NONE', #50034, 999.9999999999998863 ) ;
#132117=VECTOR ( 'NONE', #48207, 999.9999999999998863 ) ;
#132118=CARTESIAN_POINT ( 'NONE',  ( 7.499999999999951150, 5.696342897626511359, -7.587980461218381656 ) ) ;
#132119=DIRECTION ( 'NONE',  ( -0.3543493200069162685, -0.000000000000000000, -0.9351131265310288487 ) ) ;
#132120=ORIENTED_EDGE ( 'NONE', *, *, #44034, .F. ) ;
#132121=VECTOR ( 'NONE', #33533, 1000.000000000000000 ) ;
#132123=CARTESIAN_POINT ( 'NONE',  ( -6.707106781186497280, 17.25929247661554911, 5.000000000000000000 ) ) ;
#132125=CARTESIAN_POINT ( 'NONE',  ( 21.29974487139158512, -27.71228299555221142, 4.000000000000000000 ) ) ;
#132126=AXIS2_PLACEMENT_3D ( 'NONE', #6148, #29356, #50425 ) ;
#132128=CARTESIAN_POINT ( 'NONE',  ( -2.721745484314253005, 8.259292476615630818, 11.78515199841150007 ) ) ;
#132129=DIRECTION ( 'NONE',  ( 0.7071067811865486830, -0.7071067811865464625, -0.000000000000000000 ) ) ;
#132130=VERTEX_POINT ( 'NONE', #9772 ) ;
#132132=DIRECTION ( 'NONE',  ( 0.7071067811865487940, 0.7071067811865463515, -0.000000000000000000 ) ) ;
#132133=VECTOR ( 'NONE', #129830, 1000.000000000000000 ) ;
#132134=CARTESIAN_POINT ( 'NONE',  ( 75.48921356237309510, -27.52281430457107803, 5.000000000000000000 ) ) ;
#132135=ORIENTED_EDGE ( 'NONE', *, *, #37611, .T. ) ;
#132137=EDGE_CURVE ( 'NONE', #48771, #70033, #88063, .T. ) ;
#132138=LINE ( 'NONE', #32828, #124765 ) ;
#132139=FACE_OUTER_BOUND ( 'NONE', #107177, .T. ) ;
#132140=ORIENTED_EDGE ( 'NONE', *, *, #1244, .T. ) ;
#132141=DIRECTION ( 'NONE',  ( 0.7071067811865487940, -0.7071067811865463515, 0.000000000000000000 ) ) ;
#132142=LINE ( 'NONE', #42279, #44436 ) ;
#132144=AXIS2_PLACEMENT_3D ( 'NONE', #64202, #74373, #107682 ) ;
#132149=ORIENTED_EDGE ( 'NONE', *, *, #13494, .T. ) ;
#132151=AXIS2_PLACEMENT_3D ( 'NONE', #127039, #105982, #139397 ) ;
#132153=AXIS2_PLACEMENT_3D ( 'NONE', #87048, #121791, #33421 ) ;
#132154=VERTEX_POINT ( 'NONE', #101056 ) ;
#132155=LINE ( 'NONE', #21935, #110424 ) ;
#132156=CARTESIAN_POINT ( 'NONE',  ( 18.09667064187394914, -2.240707523384257716, 15.26439735382756346 ) ) ;
#132157=AXIS2_PLACEMENT_3D ( 'NONE', #24942, #80095, #98938 ) ;
#132158=ORIENTED_EDGE ( 'NONE', *, *, #71929, .F. ) ;
#132159=DIRECTION ( 'NONE',  ( -0.7071067811865486830, 0.7071067811865464625, 0.000000000000000000 ) ) ;
#132160=DIRECTION ( 'NONE',  ( 1.000000000000000000, 0.000000000000000000, 0.000000000000000000 ) ) ;
#132161=CARTESIAN_POINT ( 'NONE',  ( 8.999999999999941380, 14.96639925780211478, 5.000000000000000000 ) ) ;
#132162=CARTESIAN_POINT ( 'NONE',  ( 15.29974487139158867, -27.71228299555216879, 4.000000000000000000 ) ) ;
#132164=VECTOR ( 'NONE', #116956, 1000.000000000000000 ) ;
#132165=VERTEX_POINT ( 'NONE', #121386 ) ;
#132166=CARTESIAN_POINT ( 'NONE',  ( -34.92500000000001137, 7.701930566820932356, 4.500000000000000888 ) ) ;
#132168=CARTESIAN_POINT ( 'NONE',  ( -2.671830600776449405, 2.259292476615697876, 4.000000000000000000 ) ) ;
#132169=CARTESIAN_POINT ( 'NONE',  ( 18.18398860626898994, 28.73617430169800002, 5.000000000000000000 ) ) ;
#132170=DIRECTION ( 'NONE',  ( 0.7071067811865486830, -0.7071067811865464625, -0.000000000000000000 ) ) ;
#132175=CARTESIAN_POINT ( 'NONE',  ( -69.29974487139159578, -27.71228299555254537, 4.000000000000000000 ) ) ;
#132176=EDGE_LOOP ( 'NONE', ( #85391, #78837, #72318, #93660 ) ) ;
#132177=ORIENTED_EDGE ( 'NONE', *, *, #51338, .T. ) ;
#132179=PLANE ( 'NONE',  #41379 ) ;
#132180=VECTOR ( 'NONE', #84725, 1000.000000000000000 ) ;
#132182=ORIENTED_EDGE ( 'NONE', *, *, #8443, .T. ) ;
#132183=CARTESIAN_POINT ( 'NONE',  ( -2.345055162546169747, 5.259292476615669010, 12.77922209995893255 ) ) ;
#132184=DIRECTION ( 'NONE',  ( -0.7071067811865487940, 0.7071067811865463515, -0.000000000000000000 ) ) ;
#132186=ORIENTED_EDGE ( 'NONE', *, *, #103576, .F. ) ;
#132187=EDGE_CURVE ( 'NONE', #45797, #9933, #33700, .T. ) ;
#132188=ADVANCED_FACE ( 'NONE', ( #88792 ), #46006, .F. ) ;
#132190=ORIENTED_EDGE ( 'NONE', *, *, #110122, .T. ) ;
#132192=AXIS2_PLACEMENT_3D ( 'NONE', #108509, #111390, #99815 ) ;
#132193=DIRECTION ( 'NONE',  ( 0.7071067811865487940, 0.7071067811865463515, 0.000000000000000000 ) ) ;
#132197=PLANE ( 'NONE',  #120388 ) ;
#132198=VERTEX_POINT ( 'NONE', #54731 ) ;
#132199=LINE ( 'NONE', #21278, #39647 ) ;
#132201=EDGE_CURVE ( 'NONE', #78047, #108780, #37980, .T. ) ;
#132202=DIRECTION ( 'NONE',  ( -0.7071067811865487940, 0.7071067811865463515, 0.000000000000000000 ) ) ;
#132203=VERTEX_POINT ( 'NONE', #136542 ) ;
#132208=DIRECTION ( 'NONE',  ( -0.7071067811865487940, 0.7071067811865463515, 0.000000000000000000 ) ) ;
#132210=PLANE ( 'NONE',  #110956 ) ;
#132212=EDGE_CURVE ( 'NONE', #140579, #9125, #3850, .T. ) ;
#132213=VERTEX_POINT ( 'NONE', #26380 ) ;
#132214=CARTESIAN_POINT ( 'NONE',  ( -11.99999999999992717, 9.631307414974314085, -9.079085613539570332 ) ) ;
#132216=DIRECTION ( 'NONE',  ( 0.7071067811865487940, 0.7071067811865463515, 0.000000000000000000 ) ) ;
#132217=EDGE_CURVE ( 'NONE', #40999, #25787, #38677, .T. ) ;
#132218=DIRECTION ( 'NONE',  ( 0.3543493200069163240, -0.000000000000000000, -0.9351131265310288487 ) ) ;
#132219=DIRECTION ( 'NONE',  ( -0.6830127018922181881, 0.6830127018922202975, -0.2588190451025214056 ) ) ;
#132220=ORIENTED_EDGE ( 'NONE', *, *, #71689, .T. ) ;
#132221=ORIENTED_EDGE ( 'NONE', *, *, #77418, .F. ) ;
#132224=ORIENTED_EDGE ( 'NONE', *, *, #119757, .F. ) ;
#132225=AXIS2_PLACEMENT_3D ( 'NONE', #117755, #141703, #108302 ) ;
#132227=VECTOR ( 'NONE', #137917, 1000.000000000000000 ) ;
#132228=VERTEX_POINT ( 'NONE', #24237 ) ;
#132229=CARTESIAN_POINT ( 'NONE',  ( -13.49999999999992184, 10.08746187583916054, 4.000000000000000000 ) ) ;
#132230=ORIENTED_EDGE ( 'NONE', *, *, #73781, .T. ) ;
#132231=PLANE ( 'NONE',  #2920 ) ;
#132232=DIRECTION ( 'NONE',  ( -0.6830127018922180770, -0.6830127018922204085, -0.2588190451025213501 ) ) ;
#132233=VECTOR ( 'NONE', #34061, 1000.000000000000227 ) ;
#132234=VECTOR ( 'NONE', #119111, 1000.000000000000000 ) ;
#132236=VECTOR ( 'NONE', #31100, 1000.000000000000227 ) ;
#132237=VECTOR ( 'NONE', #72032, 1000.000000000000000 ) ;
#132238=CARTESIAN_POINT ( 'NONE',  ( -8.510786437626906675, -27.52281430457049183, 5.000000000000000000 ) ) ;
#132239=FACE_BOUND ( 'NONE', #137832, .T. ) ;
#132240=LINE ( 'NONE', #22004, #112744 ) ;
#132242=VECTOR ( 'NONE', #30911, 999.9999999999998863 ) ;
#132243=DIRECTION ( 'NONE',  ( 0.7071067811865486830, -0.7071067811865464625, -0.000000000000000000 ) ) ;
#132245=EDGE_LOOP ( 'NONE', ( #11597, #108279, #19942 ) ) ;
#132246=EDGE_CURVE ( 'NONE', #21069, #16647, #93769, .T. ) ;
#132247=PLANE ( 'NONE',  #48647 ) ;
#132249=VERTEX_POINT ( 'NONE', #13322 ) ;
#132250=ORIENTED_EDGE ( 'NONE', *, *, #35562, .F. ) ;
#132252=VERTEX_POINT ( 'NONE', #14775 ) ;
#132254=AXIS2_PLACEMENT_3D ( 'NONE', #127210, #96014, #19178 ) ;
#132255=CARTESIAN_POINT ( 'NONE',  ( 24.48921356237309510, -27.52281430457072631, 5.000000000000000000 ) ) ;
#132257=AXIS2_PLACEMENT_3D ( 'NONE', #63162, #19615, #102552 ) ;
#132258=VERTEX_POINT ( 'NONE', #48135 ) ;
#132259=LINE ( 'NONE', #33655, #109262 ) ;
#132260=VECTOR ( 'NONE', #103821, 1000.000000000000000 ) ;
#132261=CARTESIAN_POINT ( 'NONE',  ( 22.49999999999984723, -15.29013452822852415, 0.3645803511610861136 ) ) ;
#132262=ADVANCED_FACE ( 'NONE', ( #24926 ), #113359, .F. ) ;
#132263=DIRECTION ( 'NONE',  ( 0.6830127018922181881, 0.6830127018922202975, -0.2588190451025214056 ) ) ;
#132265=CARTESIAN_POINT ( 'NONE',  ( -23.29289321881329045, 20.25929247661550647, 5.000000000000000000 ) ) ;
#132266=LINE ( 'NONE', #88015, #138415 ) ;
#132267=DIRECTION ( 'NONE',  ( -0.7071067811865487940, 0.7071067811865463515, 0.000000000000000000 ) ) ;
#132269=DIRECTION ( 'NONE',  ( 0.7071067811865487940, 0.7071067811865463515, -0.000000000000000000 ) ) ;
#132270=LINE ( 'NONE', #119203, #48594 ) ;
#132271=EDGE_LOOP ( 'NONE', ( #4549, #45269, #98875, #26387 ) ) ;
#132272=CARTESIAN_POINT ( 'NONE',  ( -4.171830600776440967, 21.75929247661549937, 4.000000000000000000 ) ) ;
#132273=ORIENTED_EDGE ( 'NONE', *, *, #114544, .F. ) ;
#132274=VECTOR ( 'NONE', #37833, 999.9999999999998863 ) ;
#132278=ORIENTED_EDGE ( 'NONE', *, *, #23155, .T. ) ;
#132280=DIRECTION ( 'NONE',  ( 0.7071067811865486830, -0.7071067811865464625, -0.000000000000000000 ) ) ;
#132281=VERTEX_POINT ( 'NONE', #117619 ) ;
#132282=CARTESIAN_POINT ( 'NONE',  ( -27.08491323193744904, -12.74070752338414891, 18.74364270924348119 ) ) ;
#132284=DIRECTION ( 'NONE',  ( -0.3543493200069162685, -0.000000000000000000, -0.9351131265310288487 ) ) ;
#132285=AXIS2_PLACEMENT_3D ( 'NONE', #17876, #137565, #103472 ) ;
#132288=ORIENTED_EDGE ( 'NONE', *, *, #40757, .F. ) ;
#132289=EDGE_CURVE ( 'NONE', #105795, #7238, #141016, .T. ) ;
#132291=ORIENTED_EDGE ( 'NONE', *, *, #121644, .T. ) ;
#132293=PLANE ( 'NONE',  #45249 ) ;
#132296=VECTOR ( 'NONE', #36716, 1000.000000000000000 ) ;
#132297=EDGE_LOOP ( 'NONE', ( #88562, #97926, #31092, #83304 ) ) ;
#132299=DIRECTION ( 'NONE',  ( -0.7071067811865486830, 0.7071067811865464625, 0.000000000000000000 ) ) ;
#132300=CARTESIAN_POINT ( 'NONE',  ( 36.29974487139159578, -27.71228299555231445, 4.000000000000000000 ) ) ;
#132301=ORIENTED_EDGE ( 'NONE', *, *, #45421, .T. ) ;
#132302=ORIENTED_EDGE ( 'NONE', *, *, #21260, .T. ) ;
#132303=EDGE_CURVE ( 'NONE', #73203, #54989, #39404, .T. ) ;
#132304=ORIENTED_EDGE ( 'NONE', *, *, #29396, .F. ) ;
#132306=CARTESIAN_POINT ( 'NONE',  ( -11.16347128873443850, 15.75929247661555443, 9.299976744542897578 ) ) ;
#132307=AXIS2_PLACEMENT_3D ( 'NONE', #75078, #43853, #109083 ) ;
#132308=CARTESIAN_POINT ( 'NONE',  ( -34.92500000000001137, 21.72500000000000142, 0.4999999999999995559 ) ) ;
#132310=CARTESIAN_POINT ( 'NONE',  ( 3.083148067729290176, 21.75929247661549937, 7.311836541448058391 ) ) ;
#132311=PLANE ( 'NONE',  #81876 ) ;
#132314=DIRECTION ( 'NONE',  ( -0.7071067811865486830, -0.7071067811865464625, 0.000000000000000000 ) ) ;
#132315=ORIENTED_EDGE ( 'NONE', *, *, #29068, .F. ) ;
#132316=CARTESIAN_POINT ( 'NONE',  ( -34.42500000000001137, -19.45860074219779534, 5.000000000000000000 ) ) ;
#132317=CARTESIAN_POINT ( 'NONE',  ( 0.000000000000000000, 0.000000000000000000, 5.000000000000000000 ) ) ;
#132318=ADVANCED_FACE ( 'NONE', ( #8152 ), #61876, .F. ) ;
#132319=ORIENTED_EDGE ( 'NONE', *, *, #49699, .T. ) ;
#132320=DIRECTION ( 'NONE',  ( -0.7071067811865487940, 0.7071067811865463515, -0.000000000000000000 ) ) ;
#132321=( BOUNDED_CURVE ( )  B_SPLINE_CURVE ( 3, ( #1503, #121864, #56686, #66105 ),
 .UNSPECIFIED., .F., .T. ) 
 B_SPLINE_CURVE_WITH_KNOTS ( ( 4, 4 ),
 ( 2.001653308786173646, 3.503810798801451742 ),
 .UNSPECIFIED. ) 
 CURVE ( )  GEOMETRIC_REPRESENTATION_ITEM ( )  RATIONAL_B_SPLINE_CURVE ( ( 1.000000000000000000, 0.8206354192515249446, 0.8206354192515249446, 1.000000000000000000 ) ) 
 REPRESENTATION_ITEM ( '' )  );
#132322=FACE_OUTER_BOUND ( 'NONE', #40514, .T. ) ;
#132323=CARTESIAN_POINT ( 'NONE',  ( -63.18398860626900415, 28.73617430169831621, 5.000000000000000000 ) ) ;
#132324=ORIENTED_EDGE ( 'NONE', *, *, #72189, .F. ) ;
#132325=EDGE_CURVE ( 'NONE', #93801, #73090, #74901, .T. ) ;
#132326=LINE ( 'NONE', #53289, #44095 ) ;
#132327=FACE_OUTER_BOUND ( 'NONE', #73023, .T. ) ;
#132334=VECTOR ( 'NONE', #100335, 1000.000000000000000 ) ;
#132335=VECTOR ( 'NONE', #135944, 1000.000000000000000 ) ;
#132336=DIRECTION ( 'NONE',  ( 0.6830127018922180770, -0.6830127018922204085, -0.2588190451025213501 ) ) ;
#132337=EDGE_CURVE ( 'NONE', #43580, #32625, #119072, .T. ) ;
#132339=VERTEX_POINT ( 'NONE', #19057 ) ;
#132341=ORIENTED_EDGE ( 'NONE', *, *, #96509, .T. ) ;
#132342=VECTOR ( 'NONE', #106571, 1000.000000000000000 ) ;
#132345=LINE ( 'NONE', #77251, #66282 ) ;
#132346=AXIS2_PLACEMENT_3D ( 'NONE', #93315, #62853, #5570 ) ;
#132348=VECTOR ( 'NONE', #5584, 1000.000000000000000 ) ;
#132349=LINE ( 'NONE', #77942, #27609 ) ;
#132350=DIRECTION ( 'NONE',  ( -0.6830127018922181881, 0.6830127018922202975, -0.2588190451025214056 ) ) ;
#132351=CARTESIAN_POINT ( 'NONE',  ( 0.2997448713915885632, -27.71228299555206220, 4.000000000000000000 ) ) ;
#132352=ADVANCED_FACE ( 'NONE', ( #72058 ), #6705, .F. ) ;
#132353=CARTESIAN_POINT ( 'NONE',  ( -31.49999999999977973, -14.94781430457067906, 5.000000000000000000 ) ) ;
#132354=CARTESIAN_POINT ( 'NONE',  ( 0.000000000000000000, 0.000000000000000000, 5.000000000000000000 ) ) ;
#132359=VECTOR ( 'NONE', #77289, 1000.000000000000000 ) ;
#132360=LINE ( 'NONE', #122137, #33518 ) ;
#132363=LINE ( 'NONE', #33056, #62587 ) ;
#132365=ORIENTED_EDGE ( 'NONE', *, *, #139313, .T. ) ;
#132368=DIRECTION ( 'NONE',  ( 0.6830127018922180770, -0.6830127018922204085, -0.2588190451025213501 ) ) ;
#132369=PLANE ( 'NONE',  #124802 ) ;
#132370=CARTESIAN_POINT ( 'NONE',  ( 48.18398860626899705, 28.73617430169820608, 5.000000000000000000 ) ) ;
#132371=VERTEX_POINT ( 'NONE', #140145 ) ;
#132372=LINE ( 'NONE', #11965, #125481 ) ;
#132374=AXIS2_PLACEMENT_3D ( 'NONE', #125238, #79654, #101339 ) ;
#132375=DIRECTION ( 'NONE',  ( -0.000000000000000000, 0.3543493200069153248, 0.9351131265310292928 ) ) ;
#132377=AXIS2_PLACEMENT_3D ( 'NONE', #14572, #116738, #115260 ) ;
#132379=EDGE_LOOP ( 'NONE', ( #88458, #102236, #63432 ) ) ;
#132380=EDGE_CURVE ( 'NONE', #86945, #9815, #62580, .T. ) ;
#132382=LINE ( 'NONE', #143217, #120639 ) ;
#132383=PLANE ( 'NONE',  #142505 ) ;
#132385=LINE ( 'NONE', #54113, #13811 ) ;
#132386=PLANE ( 'NONE',  #6876 ) ;
#132387=EDGE_CURVE ( 'NONE', #120179, #128174, #96575, .T. ) ;
#132388=LINE ( 'NONE', #66394, #59181 ) ;
#132389=ORIENTED_EDGE ( 'NONE', *, *, #90278, .T. ) ;
#132390=CARTESIAN_POINT ( 'NONE',  ( -54.29974487139159578, -27.71228299555243879, 4.000000000000000000 ) ) ;
#132391=DIRECTION ( 'NONE',  ( 0.6830127018922180770, -0.6830127018922204085, -0.2588190451025213501 ) ) ;
#132392=LINE ( 'NONE', #75151, #111898 ) ;
#132393=VECTOR ( 'NONE', #120605, 1000.000000000000000 ) ;
#132394=LINE ( 'NONE', #33087, #83167 ) ;
#132395=ORIENTED_EDGE ( 'NONE', *, *, #107287, .T. ) ;
#132397=ORIENTED_EDGE ( 'NONE', *, *, #56790, .F. ) ;
#132398=EDGE_CURVE ( 'NONE', #123934, #91948, #139453, .T. ) ;
#132400=ORIENTED_EDGE ( 'NONE', *, *, #108414, .F. ) ;
#132401=EDGE_CURVE ( 'NONE', #132873, #128738, #7443, .T. ) ;
#132403=CARTESIAN_POINT ( 'NONE',  ( 11.51078643762690490, -27.52281430457047406, 5.000000000000000000 ) ) ;
#132404=LINE ( 'NONE', #77306, #41099 ) ;
#132405=EDGE_CURVE ( 'NONE', #10056, #18584, #140815, .T. ) ;
#132406=VECTOR ( 'NONE', #15347, 1000.000000000000000 ) ;
#132407=PLANE ( 'NONE',  #94359 ) ;
#132409=EDGE_LOOP ( 'NONE', ( #31208, #26861, #133243, #62700 ) ) ;
#132410=ORIENTED_EDGE ( 'NONE', *, *, #19434, .F. ) ;
#132412=EDGE_CURVE ( 'NONE', #32103, #52797, #27792, .T. ) ;
#132413=DIRECTION ( 'NONE',  ( 0.7071067811865487940, 0.7071067811865463515, -0.000000000000000000 ) ) ;
#132415=EDGE_CURVE ( 'NONE', #43467, #115656, #116233, .T. ) ;
#132416=ORIENTED_EDGE ( 'NONE', *, *, #48597, .T. ) ;
#132420=CARTESIAN_POINT ( 'NONE',  ( -28.49999999999979750, 18.05218569542898521, 5.000000000000000000 ) ) ;
#132421=AXIS2_PLACEMENT_3D ( 'NONE', #116934, #114770, #127840 ) ;
#132422=ORIENTED_EDGE ( 'NONE', *, *, #44124, .T. ) ;
#132423=EDGE_CURVE ( 'NONE', #110396, #58396, #5999, .T. ) ;
#132424=EDGE_CURVE ( 'NONE', #138243, #15180, #142288, .T. ) ;
#132425=CARTESIAN_POINT ( 'NONE',  ( -5.816011393731002066, 28.73617430169783304, 5.000000000000000000 ) ) ;
#132426=PLANE ( 'NONE',  #70957 ) ;
#132427=CARTESIAN_POINT ( 'NONE',  ( -34.92500000000001137, -3.183345613589545486, 4.500000000000000888 ) ) ;
#132428=CARTESIAN_POINT ( 'NONE',  ( -24.88837638105226446, 9.759292476615614831, 17.35367589129218402 ) ) ;
#132429=VECTOR ( 'NONE', #4601, 1000.000000000000227 ) ;
#132430=CARTESIAN_POINT ( 'NONE',  ( 8.999999999999941380, 8.587461875839151659, 4.000000000000000000 ) ) ;
#132431=EDGE_CURVE ( 'NONE', #105156, #86133, #55266, .T. ) ;
#132432=CARTESIAN_POINT ( 'NONE',  ( 39.18398860626899705, 28.73617430169814568, 5.000000000000000000 ) ) ;
#132433=ORIENTED_EDGE ( 'NONE', *, *, #44570, .F. ) ;
#132434=ORIENTED_EDGE ( 'NONE', *, *, #89335, .T. ) ;
#132436=VERTEX_POINT ( 'NONE', #32817 ) ;
#132437=ORIENTED_EDGE ( 'NONE', *, *, #22006, .T. ) ;
#132439=AXIS2_PLACEMENT_3D ( 'NONE', #140829, #98068, #142302 ) ;
#132440=VECTOR ( 'NONE', #121888, 1000.000000000000000 ) ;
#132441=DIRECTION ( 'NONE',  ( 0.7071067811865487940, -0.7071067811865463515, 0.000000000000000000 ) ) ;
#132443=LINE ( 'NONE', #74471, #118880 ) ;
#132444=VERTEX_POINT ( 'NONE', #56004 ) ;
#132445=CARTESIAN_POINT ( 'NONE',  ( 30.18398860626900060, 28.73617430169808173, 5.000000000000000000 ) ) ;
#132446=DIRECTION ( 'NONE',  ( -0.000000000000000000, -0.000000000000000000, 1.000000000000000000 ) ) ;
#132448=CARTESIAN_POINT ( 'NONE',  ( 27.32816939922334143, -3.740707523384241728, 4.000000000000000000 ) ) ;
#132449=DIRECTION ( 'NONE',  ( 1.000000000000000000, 0.000000000000000000, 0.000000000000000000 ) ) ;
#132450=EDGE_CURVE ( 'NONE', #73694, #52182, #122642, .T. ) ;
#132451=DIRECTION ( 'NONE',  ( 0.7071067811865487940, 0.7071067811865463515, 0.000000000000000000 ) ) ;
#132452=AXIS2_PLACEMENT_3D ( 'NONE', #66380, #122149, #88856 ) ;
#132453=VECTOR ( 'NONE', #142499, 1000.000000000000000 ) ;
#132456=ORIENTED_EDGE ( 'NONE', *, *, #120073, .T. ) ;
#132458=DIRECTION ( 'NONE',  ( -0.7071067811865486830, -0.7071067811865464625, 0.000000000000000000 ) ) ;
#132459=ORIENTED_EDGE ( 'NONE', *, *, #62615, .F. ) ;
#132460=VERTEX_POINT ( 'NONE', #54565 ) ;
#132464=EDGE_CURVE ( 'NONE', #28318, #11599, #100200, .T. ) ;
#132465=FACE_OUTER_BOUND ( 'NONE', #131309, .T. ) ;
#132468=CARTESIAN_POINT ( 'NONE',  ( -18.79333936457834753, 21.75929247661549937, 4.998822639870701856 ) ) ;
#132469=EDGE_CURVE ( 'NONE', #139589, #49848, #88619, .T. ) ;
#132470=LINE ( 'NONE', #54191, #24730 ) ;
#132471=ORIENTED_EDGE ( 'NONE', *, *, #91305, .F. ) ;
#132472=CARTESIAN_POINT ( 'NONE',  ( -34.92500000000001137, -22.22500000000000142, 4.000000000000000000 ) ) ;
#132473=DIRECTION ( 'NONE',  ( 0.6830127018922180770, -0.6830127018922204085, -0.2588190451025213501 ) ) ;
#132474=CARTESIAN_POINT ( 'NONE',  ( -5.999999999999963585, 19.93112307739198386, 4.000000000000000000 ) ) ;
#132476=DIRECTION ( 'NONE',  ( -0.3543493200069162685, -0.000000000000000000, -0.9351131265310288487 ) ) ;
#132479=CARTESIAN_POINT ( 'NONE',  ( 30.41161490594810601, 22.22500000000000142, 4.777194822843814137 ) ) ;
#132480=EDGE_CURVE ( 'NONE', #107805, #305, #45136, .T. ) ;
#132481=ORIENTED_EDGE ( 'NONE', *, *, #123884, .F. ) ;
#132482=AXIS2_PLACEMENT_3D ( 'NONE', #81107, #13656, #82519 ) ;
#132483=ORIENTED_EDGE ( 'NONE', *, *, #44684, .F. ) ;
#132484=ORIENTED_EDGE ( 'NONE', *, *, #104505, .T. ) ;
#132486=VECTOR ( 'NONE', #55321, 1000.000000000000000 ) ;
#132487=LINE ( 'NONE', #54210, #42326 ) ;
#132488=EDGE_CURVE ( 'NONE', #68848, #91904, #42975, .T. ) ;
#132489=DIRECTION ( 'NONE',  ( -0.000000000000000000, 0.000000000000000000, 1.000000000000000000 ) ) ;
#132490=VERTEX_POINT ( 'NONE', #132848 ) ;
#132491=CARTESIAN_POINT ( 'NONE',  ( 31.58990935480149176, 9.759292476615621936, 11.28811694763786022 ) ) ;
#132492=ORIENTED_EDGE ( 'NONE', *, *, #69926, .T. ) ;
#132493=VECTOR ( 'NONE', #130654, 1000.000000000000000 ) ;
#132495=ADVANCED_FACE ( 'NONE', ( #21905 ), #66856, .F. ) ;
#132499=ORIENTED_EDGE ( 'NONE', *, *, #123823, .T. ) ;
#132502=ORIENTED_EDGE ( 'NONE', *, *, #80980, .F. ) ;
#132503=LINE ( 'NONE', #33188, #34781 ) ;
#132506=DIRECTION ( 'NONE',  ( 0.7071067811865487940, -0.7071067811865463515, 0.000000000000000000 ) ) ;
#132507=CARTESIAN_POINT ( 'NONE',  ( -36.29974487139159578, -27.71228299555231445, 4.000000000000000000 ) ) ;
#132508=EDGE_CURVE ( 'NONE', #93492, #135550, #77038, .T. ) ;
#132509=CARTESIAN_POINT ( 'NONE',  ( 32.20710678118632586, -2.240707523384269706, 5.000000000000000000 ) ) ;
#132510=EDGE_CURVE ( 'NONE', #59483, #91502, #121213, .T. ) ;
#132511=CARTESIAN_POINT ( 'NONE',  ( 29.99451991528749417, 28.92564299267958816, 4.000000000000000000 ) ) ;
#132512=PLANE ( 'NONE',  #134384 ) ;
#132513=CARTESIAN_POINT ( 'NONE',  ( 2.816011393730999401, 28.73617430169785436, 5.000000000000000000 ) ) ;
#132514=ORIENTED_EDGE ( 'NONE', *, *, #41759, .T. ) ;
#132515=LINE ( 'NONE', #41907, #14022 ) ;
#132516=VECTOR ( 'NONE', #29049, 1000.000000000000227 ) ;
#132518=DIRECTION ( 'NONE',  ( -0.7071067811865486830, 0.7071067811865464625, 0.000000000000000000 ) ) ;
#132519=VERTEX_POINT ( 'NONE', #89314 ) ;
#132520=DIRECTION ( 'NONE',  ( 0.7071067811865487940, 0.7071067811865463515, 0.000000000000000000 ) ) ;
#132523=EDGE_CURVE ( 'NONE', #70498, #84616, #110320, .T. ) ;
#132524=CARTESIAN_POINT ( 'NONE',  ( -10.82816939922345689, 15.75929247661555799, 4.000000000000000000 ) ) ;
#132526=DIRECTION ( 'NONE',  ( 0.7071067811865487940, 0.7071067811865463515, 0.000000000000000000 ) ) ;
#132527=VECTOR ( 'NONE', #111635, 999.9999999999998863 ) ;
#132529=LINE ( 'NONE', #1918, #55962 ) ;
#132530=ORIENTED_EDGE ( 'NONE', *, *, #85365, .T. ) ;
#132531=CARTESIAN_POINT ( 'NONE',  ( -29.09565676934979450, 22.22500000000000142, 2.791043937613590931 ) ) ;
#132533=CARTESIAN_POINT ( 'NONE',  ( -14.20710678118644310, 15.75929247661555443, 5.000000000000000000 ) ) ;
#132534=DIRECTION ( 'NONE',  ( 0.7071067811865486830, -0.7071067811865464625, -0.000000000000000000 ) ) ;
#132535=LINE ( 'NONE', #35353, #123171 ) ;
#132536=CARTESIAN_POINT ( 'NONE',  ( -5.999999999999956479, 17.96639925780208458, 5.000000000000000000 ) ) ;
#132537=DIRECTION ( 'NONE',  ( 0.6830127018922181881, 0.6830127018922202975, -0.2588190451025214056 ) ) ;
#132540=VECTOR ( 'NONE', #4939, 1000.000000000000000 ) ;
#132541=VECTOR ( 'NONE', #36531, 1000.000000000000000 ) ;
#132542=VECTOR ( 'NONE', #51438, 1000.000000000000000 ) ;
#132543=LINE ( 'NONE', #10684, #95287 ) ;
#132544=CARTESIAN_POINT ( 'NONE',  ( -20.67183060077632817, -12.74070752338415247, 4.000000000000000000 ) ) ;
#132545=ORIENTED_EDGE ( 'NONE', *, *, #64471, .T. ) ;
#132546=ORIENTED_EDGE ( 'NONE', *, *, #105684, .F. ) ;
#132548=LINE ( 'NONE', #111456, #334 ) ;
#132549=EDGE_LOOP ( 'NONE', ( #111929, #3942, #117959, #133963 ) ) ;
#132550=FACE_OUTER_BOUND ( 'NONE', #111057, .T. ) ;
#132551=DIRECTION ( 'NONE',  ( 0.3543493200069163240, 0.000000000000000000, -0.9351131265310288487 ) ) ;
#132552=AXIS2_PLACEMENT_3D ( 'NONE', #54620, #64058, #98804 ) ;
#132553=DIRECTION ( 'NONE',  ( -0.7071067811865487940, 0.7071067811865463515, -0.000000000000000000 ) ) ;
#132556=PLANE ( 'NONE',  #126207 ) ;
#132559=CARTESIAN_POINT ( 'NONE',  ( -5.999999999999952927, 11.96639925780214320, 5.000000000000000000 ) ) ;
#132561=DIRECTION ( 'NONE',  ( 0.6830127018922181881, 0.6830127018922202975, -0.2588190451025214056 ) ) ;
#132562=EDGE_LOOP ( 'NONE', ( #143278, #92131, #20059, #140942 ) ) ;
#132563=CARTESIAN_POINT ( 'NONE',  ( 34.92499999999998295, -2.143876922607573121, 4.000000000000000000 ) ) ;
#132564=FACE_OUTER_BOUND ( 'NONE', #97793, .T. ) ;
#132565=CARTESIAN_POINT ( 'NONE',  ( -12.32816939922344091, 5.259292476615662792, 4.000000000000000000 ) ) ;
#132566=ORIENTED_EDGE ( 'NONE', *, *, #134580, .T. ) ;
#132567=VERTEX_POINT ( 'NONE', #34225 ) ;
#132568=VERTEX_POINT ( 'NONE', #32078 ) ;
#132569=ADVANCED_FACE ( 'NONE', ( #121913 ), #56733, .F. ) ;
#132571=ORIENTED_EDGE ( 'NONE', *, *, #54493, .T. ) ;
#132572=EDGE_CURVE ( 'NONE', #5121, #18530, #100893, .T. ) ;
#132573=CARTESIAN_POINT ( 'NONE',  ( 27.29974487139158512, -27.71228299555225405, 4.000000000000000000 ) ) ;
#132574=EDGE_CURVE ( 'NONE', #104026, #65260, #115, .T. ) ;
#132576=ORIENTED_EDGE ( 'NONE', *, *, #66331, .F. ) ;
#132577=EDGE_CURVE ( 'NONE', #60780, #97230, #98743, .T. ) ;
#132578=LINE ( 'NONE', #10036, #93033 ) ;
#132582=ORIENTED_EDGE ( 'NONE', *, *, #45723, .T. ) ;
#132583=CARTESIAN_POINT ( 'NONE',  ( -26.99999999999981171, -8.731860332648864187, -2.120594902707600315 ) ) ;
#132584=FACE_OUTER_BOUND ( 'NONE', #27886, .T. ) ;
#132585=VECTOR ( 'NONE', #87594, 999.9999999999998863 ) ;
#132586=VERTEX_POINT ( 'NONE', #9582 ) ;
#132587=VERTEX_POINT ( 'NONE', #53855 ) ;
#132589=ORIENTED_EDGE ( 'NONE', *, *, #137200, .F. ) ;
#132590=CARTESIAN_POINT ( 'NONE',  ( 0.000000000000000000, 0.000000000000000000, 5.000000000000000000 ) ) ;
#132591=EDGE_CURVE ( 'NONE', #119532, #67945, #101603, .T. ) ;
#132592=LINE ( 'NONE', #142716, #124231 ) ;
#132593=CARTESIAN_POINT ( 'NONE',  ( 57.29974487139158157, -27.71228299555246011, 4.000000000000000000 ) ) ;
#132594=DIRECTION ( 'NONE',  ( 0.7071067811865487940, 0.7071067811865463515, 0.000000000000000000 ) ) ;
#132595=EDGE_CURVE ( 'NONE', #73071, #74995, #90009, .T. ) ;
#132596=LINE ( 'NONE', #33291, #16289 ) ;
#132597=FACE_OUTER_BOUND ( 'NONE', #97254, .T. ) ;
#132598=VERTEX_POINT ( 'NONE', #2261 ) ;
#132599=EDGE_LOOP ( 'NONE', ( #110927, #131149, #119699, #113835 ) ) ;
#132600=LINE ( 'NONE', #77499, #24811 ) ;
#132602=ORIENTED_EDGE ( 'NONE', *, *, #126743, .F. ) ;
#132603=AXIS2_PLACEMENT_3D ( 'NONE', #51079, #15537, #50363 ) ;
#132604=EDGE_CURVE ( 'NONE', #138081, #99040, #82045, .T. ) ;
#132605=VECTOR ( 'NONE', #94678, 999.9999999999998863 ) ;
#132606=( BOUNDED_CURVE ( )  B_SPLINE_CURVE ( 3, ( #107926, #8595, #89768, #44149 ),
 .UNSPECIFIED., .F., .F. ) 
 B_SPLINE_CURVE_WITH_KNOTS ( ( 4, 4 ),
 ( 0.9743798061614650230, 1.027697802963069229 ),
 .UNSPECIFIED. ) 
 CURVE ( )  GEOMETRIC_REPRESENTATION_ITEM ( )  RATIONAL_B_SPLINE_CURVE ( ( 1.000000000000000000, 0.9997631132982454094, 0.9997631132982454094, 1.000000000000000000 ) ) 
 REPRESENTATION_ITEM ( '' )  );
#132607=LINE ( 'NONE', #33302, #24217 ) ;
#132608=ORIENTED_EDGE ( 'NONE', *, *, #130097, .T. ) ;
#132609=DIRECTION ( 'NONE',  ( -0.6830127018922180770, -0.6830127018922204085, -0.2588190451025213501 ) ) ;
#132611=PLANE ( 'NONE',  #108042 ) ;
#132612=EDGE_CURVE ( 'NONE', #106069, #123748, #14607, .T. ) ;
#132613=DIRECTION ( 'NONE',  ( 0.7071067811865487940, -0.7071067811865463515, 0.000000000000000000 ) ) ;
#132614=VECTOR ( 'NONE', #38237, 1000.000000000000000 ) ;
#132615=( BOUNDED_CURVE ( )  B_SPLINE_CURVE ( 3, ( #66640, #109414, #86956, #1341 ),
 .UNSPECIFIED., .F., .T. ) 
 B_SPLINE_CURVE_WITH_KNOTS ( ( 4, 4 ),
 ( 5.043186909253412509, 5.074607125596337198 ),
 .UNSPECIFIED. ) 
 CURVE ( )  GEOMETRIC_REPRESENTATION_ITEM ( )  RATIONAL_B_SPLINE_CURVE ( ( 1.000000000000000000, 0.9999177325257868620, 0.9999177325257868620, 1.000000000000000000 ) ) 
 REPRESENTATION_ITEM ( '' )  );
#132617=ORIENTED_EDGE ( 'NONE', *, *, #108560, .F. ) ;
#132618=LINE ( 'NONE', #78942, #2390 ) ;
#132619=ORIENTED_EDGE ( 'NONE', *, *, #23764, .F. ) ;
#132621=EDGE_LOOP ( 'NONE', ( #82880, #40409, #110388, #61163 ) ) ;
#132623=ORIENTED_EDGE ( 'NONE', *, *, #38759, .T. ) ;
#132624=LINE ( 'NONE', #42747, #22697 ) ;
#132625=ORIENTED_EDGE ( 'NONE', *, *, #131724, .T. ) ;
#132626=VERTEX_POINT ( 'NONE', #124792 ) ;
#132628=ORIENTED_EDGE ( 'NONE', *, *, #24175, .T. ) ;
#132629=EDGE_CURVE ( 'NONE', #41252, #135320, #58162, .T. ) ;
#132630=CARTESIAN_POINT ( 'NONE',  ( 0.1839886062690032631, 28.73617430169787568, 5.000000000000000000 ) ) ;
#132631=CARTESIAN_POINT ( 'NONE',  ( 30.79289321881324781, -2.240707523384264377, 5.000000000000000000 ) ) ;
#132632=DIRECTION ( 'NONE',  ( -0.000000000000000000, -0.3543493200069153248, -0.9351131265310292928 ) ) ;
#132633=FACE_OUTER_BOUND ( 'NONE', #91445, .T. ) ;
#132634=CARTESIAN_POINT ( 'NONE',  ( 15.00548008471250228, 28.92564299267927552, 4.000000000000000000 ) ) ;
#132635=EDGE_CURVE ( 'NONE', #89630, #113088, #81318, .T. ) ;
#132636=DIRECTION ( 'NONE',  ( -0.000000000000000000, 0.000000000000000000, 1.000000000000000000 ) ) ;
#132638=VECTOR ( 'NONE', #134256, 1000.000000000000000 ) ;
#132639=AXIS2_PLACEMENT_3D ( 'NONE', #132590, #33284, #45580 ) ;
#132640=AXIS2_PLACEMENT_3D ( 'NONE', #101, #42965, #45822 ) ;
#132641=VECTOR ( 'NONE', #15408, 1000.000000000000000 ) ;
#132643=LINE ( 'NONE', #22378, #113067 ) ;
#132644=DIRECTION ( 'NONE',  ( -0.7071067811865486830, -0.7071067811865464625, 0.000000000000000000 ) ) ;
#132645=EDGE_CURVE ( 'NONE', #64888, #28108, #113186, .T. ) ;
#132648=AXIS2_PLACEMENT_3D ( 'NONE', #34370, #55415, #31514 ) ;
#132649=EDGE_LOOP ( 'NONE', ( #134094, #129126, #99681, #8552 ) ) ;
#132650=AXIS2_PLACEMENT_3D ( 'NONE', #44086, #117502, #105223 ) ;
#132652=CARTESIAN_POINT ( 'NONE',  ( 15.50060776059232559, 22.22500000000000142, -14.10814778869267805 ) ) ;
#132653=ORIENTED_EDGE ( 'NONE', *, *, #31680, .T. ) ;
#132654=ORIENTED_EDGE ( 'NONE', *, *, #132325, .T. ) ;
#132655=CARTESIAN_POINT ( 'NONE',  ( -14.67183060077636547, 14.25929247661557042, 4.000000000000000000 ) ) ;
#132656=CARTESIAN_POINT ( 'NONE',  ( -6.792893218813409462, 9.759292476615618384, 5.000000000000000000 ) ) ;
#132657=ADVANCED_FACE ( 'NONE', ( #60279 ), #69738, .F. ) ;
#132658=CARTESIAN_POINT ( 'NONE',  ( -16.17183060077635659, 21.75929247661549581, 4.000000000000000000 ) ) ;
#132659=CARTESIAN_POINT ( 'NONE',  ( -33.18398860626899705, 28.73617430169810305, 5.000000000000000000 ) ) ;
#132660=ORIENTED_EDGE ( 'NONE', *, *, #126330, .F. ) ;
#132661=CARTESIAN_POINT ( 'NONE',  ( 25.49999999999982947, 15.05218569542901896, 5.000000000000000000 ) ) ;
#132662=ORIENTED_EDGE ( 'NONE', *, *, #104362, .F. ) ;
#132663=CARTESIAN_POINT ( 'NONE',  ( -11.81601139373100651, 28.73617430169779041, 5.000000000000000000 ) ) ;
#132666=ORIENTED_EDGE ( 'NONE', *, *, #111409, .T. ) ;
#132669=DIRECTION ( 'NONE',  ( -0.7071067811865486830, -0.7071067811865464625, 0.000000000000000000 ) ) ;
#132671=ORIENTED_EDGE ( 'NONE', *, *, #19218, .T. ) ;
#132672=CARTESIAN_POINT ( 'NONE',  ( -4.499999999999968914, 10.94296225409026668, -9.576120664313268804 ) ) ;
#132673=ORIENTED_EDGE ( 'NONE', *, *, #42022, .F. ) ;
#132675=LINE ( 'NONE', #77566, #114359 ) ;
#132676=CARTESIAN_POINT ( 'NONE',  ( 34.17183060077623225, 15.75929247661556687, 4.000000000000000000 ) ) ;
#132678=DIRECTION ( 'NONE',  ( 0.6830127018922180770, -0.6830127018922204085, -0.2588190451025213501 ) ) ;
#132679=CARTESIAN_POINT ( 'NONE',  ( 34.82816939922328459, -14.24070752338414714, 4.000000000000000000 ) ) ;
#132680=VERTEX_POINT ( 'NONE', #47295 ) ;
#132683=EDGE_CURVE ( 'NONE', #10836, #120276, #71150, .T. ) ;
#132684=VECTOR ( 'NONE', #143145, 1000.000000000000227 ) ;
#132685=DIRECTION ( 'NONE',  ( -1.000000000000000000, 0.000000000000000000, 0.000000000000000000 ) ) ;
#132686=DIRECTION ( 'NONE',  ( 1.000000000000000000, 0.000000000000000000, 0.000000000000000000 ) ) ;
#132687=ORIENTED_EDGE ( 'NONE', *, *, #133227, .F. ) ;
#132688=DIRECTION ( 'NONE',  ( -0.000000000000000000, -0.000000000000000000, 1.000000000000000000 ) ) ;
#132690=LINE ( 'NONE', #53680, #58670 ) ;
#132691=ORIENTED_EDGE ( 'NONE', *, *, #134931, .F. ) ;
#132692=EDGE_CURVE ( 'NONE', #57534, #124891, #3006, .T. ) ;
#132693=CARTESIAN_POINT ( 'NONE',  ( -21.29974487139158512, -27.71228299555221142, 4.000000000000000000 ) ) ;
#132694=ORIENTED_EDGE ( 'NONE', *, *, #47193, .T. ) ;
#132695=EDGE_LOOP ( 'NONE', ( #65898, #45012, #67786, #116799, #120382, #125514 ) ) ;
#132696=EDGE_CURVE ( 'NONE', #112107, #50934, #92145, .T. ) ;
#132697=LINE ( 'NONE', #77585, #21522 ) ;
#132698=CARTESIAN_POINT ( 'NONE',  ( -5.292986735706916690, -21.74070752338406010, 4.999753212805220670 ) ) ;
#132699=VERTEX_POINT ( 'NONE', #59566 ) ;
#132701=VECTOR ( 'NONE', #113751, 1000.000000000000227 ) ;
#132702=DIRECTION ( 'NONE',  ( 0.6830127018922181881, 0.6830127018922202975, -0.2588190451025214056 ) ) ;
#132703=DIRECTION ( 'NONE',  ( -0.7071067811865486830, -0.7071067811865464625, 0.000000000000000000 ) ) ;
#132704=CARTESIAN_POINT ( 'NONE',  ( -18.18398860626898994, 28.73617430169800002, 5.000000000000000000 ) ) ;
#132705=LINE ( 'NONE', #57278, #81585 ) ;
#132707=CARTESIAN_POINT ( 'NONE',  ( 54.18398860626899705, 28.73617430169825226, 5.000000000000000000 ) ) ;
#132708=CARTESIAN_POINT ( 'NONE',  ( 34.17183060077623225, -11.24070752338416490, 4.000000000000000000 ) ) ;
#132710=DIRECTION ( 'NONE',  ( -0.7071067811865487940, 0.7071067811865463515, 0.000000000000000000 ) ) ;
#132711=AXIS2_PLACEMENT_3D ( 'NONE', #79431, #123628, #80123 ) ;
#132712=DIRECTION ( 'NONE',  ( -0.7071067811865486830, -0.7071067811865464625, -0.000000000000000000 ) ) ;
#132713=CARTESIAN_POINT ( 'NONE',  ( -1.889826771117871784, -22.22500000000000142, 4.785647885939354751 ) ) ;
#132714=PLANE ( 'NONE',  #10623 ) ;
#132715=VERTEX_POINT ( 'NONE', #137106 ) ;
#132716=EDGE_CURVE ( 'NONE', #15253, #36181, #26206, .T. ) ;
#132717=ORIENTED_EDGE ( 'NONE', *, *, #132380, .F. ) ;
#132719=ORIENTED_EDGE ( 'NONE', *, *, #107033, .F. ) ;
#132720=ORIENTED_EDGE ( 'NONE', *, *, #44794, .T. ) ;
#132721=ORIENTED_EDGE ( 'NONE', *, *, #24336, .F. ) ;
#132722=LINE ( 'NONE', #58014, #122018 ) ;
#132723=DIRECTION ( 'NONE',  ( -0.000000000000000000, -0.000000000000000000, 1.000000000000000000 ) ) ;
#132724=VECTOR ( 'NONE', #136710, 1000.000000000000227 ) ;
#132726=LINE ( 'NONE', #121785, #27823 ) ;
#132728=FACE_OUTER_BOUND ( 'NONE', #84154, .T. ) ;
#132729=DIRECTION ( 'NONE',  ( -0.6830127018922181881, 0.6830127018922202975, -0.2588190451025214056 ) ) ;
#132730=VERTEX_POINT ( 'NONE', #114614 ) ;
#132732=LINE ( 'NONE', #100780, #25934 ) ;
#132733=DIRECTION ( 'NONE',  ( 0.3543493200069163240, -0.000000000000000000, 0.9351131265310288487 ) ) ;
#132736=DIRECTION ( 'NONE',  ( -0.7071067811865486830, 0.7071067811865464625, 0.000000000000000000 ) ) ;
#132738=ORIENTED_EDGE ( 'NONE', *, *, #44198, .T. ) ;
#132739=EDGE_CURVE ( 'NONE', #47092, #140803, #79914, .T. ) ;
#132741=VERTEX_POINT ( 'NONE', #92871 ) ;
#132742=EDGE_CURVE ( 'NONE', #79780, #50223, #69008, .T. ) ;
#132743=CARTESIAN_POINT ( 'NONE',  ( -34.92500000000001137, -16.48753812416032360, 4.000000000000000000 ) ) ;
#132745=CARTESIAN_POINT ( 'NONE',  ( 17.99451991528748351, 28.92564299267950645, 4.000000000000000000 ) ) ;
#132746=EDGE_CURVE ( 'NONE', #139884, #69443, #104456, .T. ) ;
#132747=EDGE_CURVE ( 'NONE', #136709, #19349, #36369, .T. ) ;
#132748=DIRECTION ( 'NONE',  ( -0.000000000000000000, -0.3543493200069152693, 0.9351131265310292928 ) ) ;
#132750=VECTOR ( 'NONE', #49371, 1000.000000000000227 ) ;
#132752=ORIENTED_EDGE ( 'NONE', *, *, #64279, .F. ) ;
#132753=VERTEX_POINT ( 'NONE', #134991 ) ;
#132754=VECTOR ( 'NONE', #78521, 1000.000000000000000 ) ;
#132755=DIRECTION ( 'NONE',  ( -0.7071067811865486830, -0.7071067811865464625, 0.000000000000000000 ) ) ;
#132758=ORIENTED_EDGE ( 'NONE', *, *, #11227, .F. ) ;
#132759=ORIENTED_EDGE ( 'NONE', *, *, #8960, .T. ) ;
#132761=EDGE_CURVE ( 'NONE', #77764, #8795, #80597, .T. ) ;
#132762=VERTEX_POINT ( 'NONE', #39222 ) ;
#132763=CARTESIAN_POINT ( 'NONE',  ( 9.183988606268997046, 28.73617430169793607, 5.000000000000000000 ) ) ;
#132764=EDGE_CURVE ( 'NONE', #82496, #38440, #50104, .T. ) ;
#132765=CARTESIAN_POINT ( 'NONE',  ( 34.42499999999998295, -22.22500000000000142, 4.500000000000000888 ) ) ;
#132766=VECTOR ( 'NONE', #63161, 1000.000000000000227 ) ;
#132769=EDGE_LOOP ( 'NONE', ( #55858, #44402, #17288 ) ) ;
#132770=DIRECTION ( 'NONE',  ( 0.6830127018922180770, -0.6830127018922204085, -0.2588190451025213501 ) ) ;
#132772=ORIENTED_EDGE ( 'NONE', *, *, #77784, .F. ) ;
#132773=EDGE_CURVE ( 'NONE', #15499, #77121, #105867, .T. ) ;
#132774=ORIENTED_EDGE ( 'NONE', *, *, #47014, .T. ) ;
#132777=LINE ( 'NONE', #55916, #92780 ) ;
#132778=VERTEX_POINT ( 'NONE', #62413 ) ;
#132779=AXIS2_PLACEMENT_3D ( 'NONE', #137751, #91396, #70388 ) ;
#132780=CARTESIAN_POINT ( 'NONE',  ( -29.20710678118634007, -2.240707523384255939, 5.000000000000000000 ) ) ;
#132781=EDGE_CURVE ( 'NONE', #94514, #88116, #72610, .T. ) ;
#132782=DIRECTION ( 'NONE',  ( -0.000000000000000000, 0.3543493200069153248, 0.9351131265310292928 ) ) ;
#132783=VECTOR ( 'NONE', #34394, 1000.000000000000227 ) ;
#132784=FACE_BOUND ( 'NONE', #50131, .T. ) ;
#132785=ORIENTED_EDGE ( 'NONE', *, *, #82385, .F. ) ;
#132786=LINE ( 'NONE', #122570, #17907 ) ;
#132787=DIRECTION ( 'NONE',  ( 0.7071067811865487940, 0.7071067811865463515, -0.000000000000000000 ) ) ;
#132788=CARTESIAN_POINT ( 'NONE',  ( -21.48921356237309155, -27.52281430457070499, 5.000000000000000000 ) ) ;
#132790=ADVANCED_FACE ( 'NONE', ( #74726 ), #63839, .F. ) ;
#132791=DIRECTION ( 'NONE',  ( 1.000000000000000000, 0.000000000000000000, 0.000000000000000000 ) ) ;
#132792=VERTEX_POINT ( 'NONE', #96411 ) ;
#132793=EDGE_CURVE ( 'NONE', #67347, #115536, #29052, .T. ) ;
#132794=ORIENTED_EDGE ( 'NONE', *, *, #67966, .T. ) ;
#132795=( BOUNDED_CURVE ( )  B_SPLINE_CURVE ( 3, ( #19446, #22269, #30325, #63695 ),
 .UNSPECIFIED., .F., .T. ) 
 B_SPLINE_CURVE_WITH_KNOTS ( ( 4, 4 ),
 ( 2.001653308786165208, 3.503810798801451742 ),
 .UNSPECIFIED. ) 
 CURVE ( )  GEOMETRIC_REPRESENTATION_ITEM ( )  RATIONAL_B_SPLINE_CURVE ( ( 1.000000000000000000, 0.8206354192515228352, 0.8206354192515228352, 1.000000000000000000 ) ) 
 REPRESENTATION_ITEM ( '' )  );
#132800=VECTOR ( 'NONE', #49030, 1000.000000000000000 ) ;
#132801=ORIENTED_EDGE ( 'NONE', *, *, #132415, .T. ) ;
#132802=AXIS2_PLACEMENT_3D ( 'NONE', #48541, #136978, #16607 ) ;
#132803=LINE ( 'NONE', #142924, #37136 ) ;
#132804=DIRECTION ( 'NONE',  ( -0.6830127018922180770, -0.6830127018922204085, -0.2588190451025213501 ) ) ;
#132805=PLANE ( 'NONE',  #125150 ) ;
#132808=LINE ( 'NONE', #33489, #119905 ) ;
#132810=FACE_OUTER_BOUND ( 'NONE', #79693, .T. ) ;
#132811=DIRECTION ( 'NONE',  ( -0.6830127018922181881, 0.6830127018922202975, -0.2588190451025214056 ) ) ;
#132813=VERTEX_POINT ( 'NONE', #117458 ) ;
#132814=VECTOR ( 'NONE', #128015, 1000.000000000000000 ) ;
#132815=VERTEX_POINT ( 'NONE', #137831 ) ;
#132816=VERTEX_POINT ( 'NONE', #63141 ) ;
#132817=DIRECTION ( 'NONE',  ( 0.7071067811865487940, 0.7071067811865463515, 0.000000000000000000 ) ) ;
#132818=FACE_OUTER_BOUND ( 'NONE', #108038, .T. ) ;
#132819=ORIENTED_EDGE ( 'NONE', *, *, #138540, .T. ) ;
#132820=EDGE_LOOP ( 'NONE', ( #123343, #9136, #68282, #84674 ) ) ;
#132821=CARTESIAN_POINT ( 'NONE',  ( -9.183988606268997046, 28.73617430169793607, 5.000000000000000000 ) ) ;
#132822=DIRECTION ( 'NONE',  ( -0.000000000000000000, 0.3543493200069153248, 0.9351131265310292928 ) ) ;
#132823=DIRECTION ( 'NONE',  ( -0.7071067811865486830, -0.7071067811865464625, 0.000000000000000000 ) ) ;
#132824=VECTOR ( 'NONE', #58416, 1000.000000000000000 ) ;
#132825=ORIENTED_EDGE ( 'NONE', *, *, #48574, .F. ) ;
#132826=CARTESIAN_POINT ( 'NONE',  ( -7.499999999999951150, -14.70932175296478128, -11.46312253303835504 ) ) ;
#132829=VECTOR ( 'NONE', #106349, 1000.000000000000000 ) ;
#132831=VERTEX_POINT ( 'NONE', #27608 ) ;
#132833=DIRECTION ( 'NONE',  ( -0.000000000000000000, 0.3543493200069153248, 0.9351131265310292928 ) ) ;
#132834=DIRECTION ( 'NONE',  ( -0.000000000000000000, 0.3543493200069153248, 0.9351131265310292928 ) ) ;
#132835=CARTESIAN_POINT ( 'NONE',  ( 19.05000000000000071, 3.174999999999997158, 5.000000000000000000 ) ) ;
#132836=ORIENTED_EDGE ( 'NONE', *, *, #115263, .F. ) ;
#132837=LINE ( 'NONE', #121900, #39303 ) ;
#132838=ORIENTED_EDGE ( 'NONE', *, *, #11756, .F. ) ;
#132839=LINE ( 'NONE', #54557, #81726 ) ;
#132840=CARTESIAN_POINT ( 'NONE',  ( -23.99999999999983302, -15.03360074219758502, 5.000000000000000000 ) ) ;
#132841=VECTOR ( 'NONE', #142579, 1000.000000000000000 ) ;
#132842=ORIENTED_EDGE ( 'NONE', *, *, #53758, .T. ) ;
#132843=DIRECTION ( 'NONE',  ( -0.000000000000000000, -0.000000000000000000, 1.000000000000000000 ) ) ;
#132845=ORIENTED_EDGE ( 'NONE', *, *, #64784, .T. ) ;
#132847=CARTESIAN_POINT ( 'NONE',  ( -2.816011393730999401, 28.73617430169785436, 5.000000000000000000 ) ) ;
#132848=CARTESIAN_POINT ( 'NONE',  ( -5.999999999999950262, 8.966399257802171618, 5.000000000000000000 ) ) ;
#132849=ORIENTED_EDGE ( 'NONE', *, *, #127156, .F. ) ;
#132850=LINE ( 'NONE', #22590, #73904 ) ;
#132851=EDGE_CURVE ( 'NONE', #10224, #85316, #38506, .T. ) ;
#132852=DIRECTION ( 'NONE',  ( 1.000000000000000000, 0.000000000000000000, 0.000000000000000000 ) ) ;
#132853=EDGE_LOOP ( 'NONE', ( #127780, #140610, #96860, #80463 ) ) ;
#132854=ADVANCED_FACE ( 'NONE', ( #82730 ), #139271, .F. ) ;
#132855=ORIENTED_EDGE ( 'NONE', *, *, #21095, .F. ) ;
#132856=CARTESIAN_POINT ( 'NONE',  ( 33.51665438641022376, 22.22500000000000142, 4.500000000000000888 ) ) ;
#132858=EDGE_LOOP ( 'NONE', ( #105036, #11656, #59866, #5779 ) ) ;
#132860=VECTOR ( 'NONE', #140501, 999.9999999999998863 ) ;
#132861=DIRECTION ( 'NONE',  ( -0.7071067811865486830, -0.7071067811865464625, -0.000000000000000000 ) ) ;
#132863=ORIENTED_EDGE ( 'NONE', *, *, #17929, .T. ) ;
#132864=EDGE_CURVE ( 'NONE', #120303, #59180, #126908, .T. ) ;
#132865=PLANE ( 'NONE',  #134645 ) ;
#132866=CARTESIAN_POINT ( 'NONE',  ( -60.48921356237309510, -27.52281430457097500, 5.000000000000000000 ) ) ;
#132867=CARTESIAN_POINT ( 'NONE',  ( -21.29974487139158512, -27.71228299555221142, 4.000000000000000000 ) ) ;
#132870=VECTOR ( 'NONE', #90170, 1000.000000000000000 ) ;
#132872=EDGE_CURVE ( 'NONE', #71242, #105060, #127663, .T. ) ;
#132873=VERTEX_POINT ( 'NONE', #16743 ) ;
#132874=EDGE_LOOP ( 'NONE', ( #138705, #122247, #97161, #110293 ) ) ;
#132876=VECTOR ( 'NONE', #24052, 1000.000000000000000 ) ;
#132877=ORIENTED_EDGE ( 'NONE', *, *, #61807, .T. ) ;
#132878=AXIS2_PLACEMENT_3D ( 'NONE', #98123, #87950, #132193 ) ;
#132879=ORIENTED_EDGE ( 'NONE', *, *, #58518, .T. ) ;
#132880=LINE ( 'NONE', #102388, #40921 ) ;
#132881=CARTESIAN_POINT ( 'NONE',  ( 32.29289321881321939, 11.25929247661560062, 5.000000000000000000 ) ) ;
#132884=FACE_OUTER_BOUND ( 'NONE', #92224, .T. ) ;
#132886=AXIS2_PLACEMENT_3D ( 'NONE', #95902, #105346, #61877 ) ;
#132887=DIRECTION ( 'NONE',  ( -0.6830127018922181881, 0.6830127018922202975, -0.2588190451025214056 ) ) ;
#132889=LINE ( 'NONE', #122679, #102070 ) ;
#132892=CARTESIAN_POINT ( 'NONE',  ( -54.48921356237310221, -27.52281430457093236, 5.000000000000000000 ) ) ;
#132893=CARTESIAN_POINT ( 'NONE',  ( 13.88982677111779473, -22.22500000000000142, 4.785647885939352086 ) ) ;
#132894=EDGE_CURVE ( 'NONE', #142445, #7871, #105176, .T. ) ;
#132895=DIRECTION ( 'NONE',  ( -0.7071067811865487940, 0.7071067811865463515, 0.000000000000000000 ) ) ;
#132897=DIRECTION ( 'NONE',  ( -0.6830127018922181881, 0.6830127018922202975, -0.2588190451025214056 ) ) ;
#132898=FACE_OUTER_BOUND ( 'NONE', #56499, .T. ) ;
#132899=DIRECTION ( 'NONE',  ( -0.6830127018922180770, -0.6830127018922204085, -0.2588190451025213501 ) ) ;
#132900=VECTOR ( 'NONE', #138482, 1000.000000000000000 ) ;
#132902=LINE ( 'NONE', #1600, #134752 ) ;
#132903=AXIS2_PLACEMENT_3D ( 'NONE', #64496, #84821, #116735 ) ;
#132904=CARTESIAN_POINT ( 'NONE',  ( 42.18398860626899705, 28.73617430169816700, 5.000000000000000000 ) ) ;
#132905=ORIENTED_EDGE ( 'NONE', *, *, #66737, .F. ) ;
#132906=ORIENTED_EDGE ( 'NONE', *, *, #4499, .T. ) ;
#132908=CARTESIAN_POINT ( 'NONE',  ( 59.99451991528749772, 28.92564299267980132, 4.000000000000000000 ) ) ;
#132909=EDGE_CURVE ( 'NONE', #111254, #13885, #7265, .T. ) ;
#132910=AXIS2_PLACEMENT_3D ( 'NONE', #56398, #44813, #25858 ) ;
#132911=DIRECTION ( 'NONE',  ( -0.7071067811865486830, -0.7071067811865464625, 0.000000000000000000 ) ) ;
#132912=VERTEX_POINT ( 'NONE', #51538 ) ;
#132914=DIRECTION ( 'NONE',  ( 0.3543493200069163795, -9.265275131829747941E-33, -0.9351131265310288487 ) ) ;
#132915=EDGE_CURVE ( 'NONE', #88412, #60505, #84183, .T. ) ;
#132916=ADVANCED_FACE ( 'NONE', ( #107316 ), #7985, .F. ) ;
#132918=EDGE_LOOP ( 'NONE', ( #88454, #120940, #26983, #74631 ) ) ;
#132919=CARTESIAN_POINT ( 'NONE',  ( -34.42500000000001137, -4.458600742197945443, 5.000000000000000000 ) ) ;
#132920=ORIENTED_EDGE ( 'NONE', *, *, #123194, .T. ) ;
#132921=ORIENTED_EDGE ( 'NONE', *, *, #33697, .T. ) ;
#132923=CARTESIAN_POINT ( 'NONE',  ( 13.98012225071443915, -17.24070752338409918, 20.23474786156472405 ) ) ;
#132924=EDGE_CURVE ( 'NONE', #33315, #18584, #110854, .T. ) ;
#132925=FACE_OUTER_BOUND ( 'NONE', #21493, .T. ) ;
#132927=DIRECTION ( 'NONE',  ( 0.7071067811865487940, 0.7071067811865463515, 0.000000000000000000 ) ) ;
#132928=ORIENTED_EDGE ( 'NONE', *, *, #35190, .F. ) ;
#132929=ADVANCED_FACE ( 'NONE', ( #54405 ), #87713, .F. ) ;
#132930=DIRECTION ( 'NONE',  ( 0.7071067811865487940, 0.7071067811865463515, -0.000000000000000000 ) ) ;
#132933=ADVANCED_FACE ( 'NONE', ( #34066 ), #52913, .F. ) ;
#132934=CARTESIAN_POINT ( 'NONE',  ( -12.70710678118644843, -12.74070752338415602, 5.000000000000000000 ) ) ;
#132935=DIRECTION ( 'NONE',  ( 0.7071067811865487940, 0.7071067811865463515, 0.000000000000000000 ) ) ;
#132936=DIRECTION ( 'NONE',  ( -0.7071067811865486830, -0.7071067811865464625, -0.000000000000000000 ) ) ;
#132937=VERTEX_POINT ( 'NONE', #141377 ) ;
#132938=AXIS2_PLACEMENT_3D ( 'NONE', #59030, #5977, #38655 ) ;
#132939=EDGE_CURVE ( 'NONE', #85156, #33404, #44978, .T. ) ;
#132940=DIRECTION ( 'NONE',  ( -0.7071067811865486830, -0.7071067811865464625, 0.000000000000000000 ) ) ;
#132942=DIRECTION ( 'NONE',  ( -0.7071067811865486830, -0.7071067811865464625, 0.000000000000000000 ) ) ;
#132943=DIRECTION ( 'NONE',  ( 0.7071067811865487940, -0.7071067811865463515, 0.000000000000000000 ) ) ;
#132944=CARTESIAN_POINT ( 'NONE',  ( -34.42500000000001137, -22.22500000000000142, 5.000000000000000000 ) ) ;
#132945=ORIENTED_EDGE ( 'NONE', *, *, #113381, .T. ) ;
#132946=VERTEX_POINT ( 'NONE', #43497 ) ;
#132949=ADVANCED_FACE ( 'NONE', ( #89152 ), #86997, .F. ) ;
#132950=ORIENTED_EDGE ( 'NONE', *, *, #101956, .T. ) ;
#132951=VECTOR ( 'NONE', #89603, 1000.000000000000000 ) ;
#132953=ORIENTED_EDGE ( 'NONE', *, *, #13063, .T. ) ;
#132954=LINE ( 'NONE', #9695, #104759 ) ;
#132955=PLANE ( 'NONE',  #124364 ) ;
#132956=CARTESIAN_POINT ( 'NONE',  ( 17.99999999999987566, 16.93112307739200872, 4.000000000000000000 ) ) ;
#132957=FACE_BOUND ( 'NONE', #94879, .T. ) ;
#132959=CARTESIAN_POINT ( 'NONE',  ( 5.816011393731002066, 28.73617430169783304, 5.000000000000000000 ) ) ;
#132960=DIRECTION ( 'NONE',  ( -0.3543493200069162685, -0.000000000000000000, -0.9351131265310288487 ) ) ;
#132961=FACE_OUTER_BOUND ( 'NONE', #8551, .T. ) ;
#132962=EDGE_LOOP ( 'NONE', ( #81883, #97125, #62195, #42289 ) ) ;
#132963=AXIS2_PLACEMENT_3D ( 'NONE', #96180, #98365, #117920 ) ;
#132966=EDGE_CURVE ( 'NONE', #84862, #1609, #119596, .T. ) ;
#132968=VECTOR ( 'NONE', #25144, 999.9999999999998863 ) ;
#132971=VERTEX_POINT ( 'NONE', #42807 ) ;
#132972=DIRECTION ( 'NONE',  ( 0.7071067811865487940, -0.7071067811865463515, 0.000000000000000000 ) ) ;
#132973=LINE ( 'NONE', #20586, #44395 ) ;
#132977=LINE ( 'NONE', #58295, #58828 ) ;
#132978=CARTESIAN_POINT ( 'NONE',  ( 18.48921356237309510, -27.52281430457068367, 5.000000000000000000 ) ) ;
#132979=CARTESIAN_POINT ( 'NONE',  ( 3.770042794577902256, 21.73644205237997440, 5.000000000000000888 ) ) ;
#132980=VECTOR ( 'NONE', #53479, 999.9999999999998863 ) ;
#132981=CARTESIAN_POINT ( 'NONE',  ( -30.29974487139158867, -27.71228299555227537, 4.000000000000000000 ) ) ;
#132982=DIRECTION ( 'NONE',  ( 0.3543493200069162685, -0.000000000000000000, -0.9351131265310288487 ) ) ;
#132983=CARTESIAN_POINT ( 'NONE',  ( 15.18398860626900237, 28.73617430169797871, 5.000000000000000000 ) ) ;
#132985=LINE ( 'NONE', #36321, #39955 ) ;
#132986=ORIENTED_EDGE ( 'NONE', *, *, #103889, .F. ) ;
#132987=LINE ( 'NONE', #43807, #58683 ) ;
#132989=ORIENTED_EDGE ( 'NONE', *, *, #92256, .F. ) ;
#132991=VERTEX_POINT ( 'NONE', #131950 ) ;
#132992=VECTOR ( 'NONE', #69353, 1000.000000000000000 ) ;
#132993=LINE ( 'NONE', #43813, #4436 ) ;
#132994=ORIENTED_EDGE ( 'NONE', *, *, #124173, .T. ) ;
#132996=AXIS2_PLACEMENT_3D ( 'NONE', #129042, #29714, #73964 ) ;
#132997=LINE ( 'NONE', #21349, #97952 ) ;
#132998=AXIS2_PLACEMENT_3D ( 'NONE', #50598, #51323, #43127 ) ;
#133000=DIRECTION ( 'NONE',  ( 0.6830127018922181881, 0.6830127018922202975, -0.2588190451025214056 ) ) ;
#133001=ORIENTED_EDGE ( 'NONE', *, *, #23951, .T. ) ;
#133002=ORIENTED_EDGE ( 'NONE', *, *, #137186, .F. ) ;
#133003=LINE ( 'NONE', #109787, #23318 ) ;
#133004=DIRECTION ( 'NONE',  ( -0.000000000000000000, -0.000000000000000000, 1.000000000000000000 ) ) ;
#133005=CARTESIAN_POINT ( 'NONE',  ( 0.005480084712502889671, 28.92564299267938210, 4.000000000000000000 ) ) ;
#133006=VERTEX_POINT ( 'NONE', #76132 ) ;
#133007=VERTEX_POINT ( 'NONE', #131220 ) ;
#133008=CARTESIAN_POINT ( 'NONE',  ( 42.29974487139158157, -27.71228299555235708, 4.000000000000000000 ) ) ;
#133009=( BOUNDED_CURVE ( )  B_SPLINE_CURVE ( 3, ( #58823, #25398, #102291, #47234 ),
 .UNSPECIFIED., .F., .F. ) 
 B_SPLINE_CURVE_WITH_KNOTS ( ( 4, 4 ),
 ( 1.208578181583233491, 1.359146454359404510 ),
 .UNSPECIFIED. ) 
 CURVE ( )  GEOMETRIC_REPRESENTATION_ITEM ( )  RATIONAL_B_SPLINE_CURVE ( ( 1.000000000000000000, 0.9981116584018959736, 0.9981116584018959736, 1.000000000000000000 ) ) 
 REPRESENTATION_ITEM ( '' )  );
#133010=LINE ( 'NONE', #111197, #90828 ) ;
#133011=DIRECTION ( 'NONE',  ( 0.7071067811865486830, -0.7071067811865464625, -0.000000000000000000 ) ) ;
#133012=ORIENTED_EDGE ( 'NONE', *, *, #132939, .T. ) ;
#133014=LINE ( 'NONE', #39752, #73403 ) ;
#133015=ORIENTED_EDGE ( 'NONE', *, *, #55162, .T. ) ;
#133017=LINE ( 'NONE', #3168, #21638 ) ;
#133018=DIRECTION ( 'NONE',  ( 0.6830127018922181881, 0.6830127018922202975, -0.2588190451025214056 ) ) ;
#133019=CARTESIAN_POINT ( 'NONE',  ( -4.228506771386627783, 20.25929247661551003, 7.808871592221759528 ) ) ;
#133020=FACE_OUTER_BOUND ( 'NONE', #125530, .T. ) ;
#133021=ADVANCED_FACE ( 'NONE', ( #9395 ), #97114, .F. ) ;
#133023=DIRECTION ( 'NONE',  ( -0.7071067811865486830, -0.7071067811865464625, -0.000000000000000000 ) ) ;
#133024=ADVANCED_FACE ( 'NONE', ( #86305 ), #32638, .F. ) ;
#133025=EDGE_CURVE ( 'NONE', #115355, #67593, #75423, .T. ) ;
#133026=ORIENTED_EDGE ( 'NONE', *, *, #28065, .F. ) ;
#133027=ORIENTED_EDGE ( 'NONE', *, *, #107591, .F. ) ;
#133030=EDGE_CURVE ( 'NONE', #54989, #115943, #130526, .T. ) ;
#133031=EDGE_CURVE ( 'NONE', #12969, #96758, #44233, .T. ) ;
#133033=ORIENTED_EDGE ( 'NONE', *, *, #50225, .T. ) ;
#133034=DIRECTION ( 'NONE',  ( 0.7071067811865487940, 0.7071067811865463515, -0.000000000000000000 ) ) ;
#133035=CARTESIAN_POINT ( 'NONE',  ( -12.09843580608229274, 11.25929247661560950, 10.79108189686404096 ) ) ;
#133037=EDGE_CURVE ( 'NONE', #133264, #69882, #132690, .T. ) ;
#133039=DIRECTION ( 'NONE',  ( 0.6830127018922180770, -0.6830127018922204085, -0.2588190451025213501 ) ) ;
#133040=CARTESIAN_POINT ( 'NONE',  ( 20.81601139373100295, 28.73617430169773002, 5.000000000000000000 ) ) ;
#133042=DIRECTION ( 'NONE',  ( 0.7071067811865487940, -0.7071067811865463515, 0.000000000000000000 ) ) ;
#133045=LINE ( 'NONE', #90959, #97327 ) ;
#133046=ADVANCED_FACE ( 'NONE', ( #65997 ), #66687, .F. ) ;
#133047=CARTESIAN_POINT ( 'NONE',  ( 28.17183060077627488, -20.24070752338407431, 4.000000000000000000 ) ) ;
#133049=DIRECTION ( 'NONE',  ( -0.000000000000000000, -0.3543493200069152693, 0.9351131265310292928 ) ) ;
#133050=ORIENTED_EDGE ( 'NONE', *, *, #14401, .F. ) ;
#133052=ORIENTED_EDGE ( 'NONE', *, *, #100127, .T. ) ;
#133053=CARTESIAN_POINT ( 'NONE',  ( 17.84387692260747116, -22.22499999999999076, 4.000000000000000000 ) ) ;
#133054=ADVANCED_FACE ( 'NONE', ( #112330 ), #126066, .F. ) ;
#133055=CARTESIAN_POINT ( 'NONE',  ( 42.48921356237308800, -27.52281430457085065, 5.000000000000000000 ) ) ;
#133056=DIRECTION ( 'NONE',  ( 0.6830127018922180770, -0.6830127018922204085, -0.2588190451025213501 ) ) ;
#133058=CARTESIAN_POINT ( 'NONE',  ( -34.47516574401893052, 13.49051761211547529, 4.998110765256835286 ) ) ;
#133059=PLANE ( 'NONE',  #59304 ) ;
#133061=ORIENTED_EDGE ( 'NONE', *, *, #75745, .F. ) ;
#133062=CARTESIAN_POINT ( 'NONE',  ( 5.816011393731002066, 28.73617430169783304, 5.000000000000000000 ) ) ;
#133063=DIRECTION ( 'NONE',  ( -0.6830127018922181881, 0.6830127018922202975, -0.2588190451025214056 ) ) ;
#133066=EDGE_CURVE ( 'NONE', #63744, #70033, #12981, .T. ) ;
#133067=DIRECTION ( 'NONE',  ( 0.7071067811865487940, -0.7071067811865463515, -0.000000000000000000 ) ) ;
#133068=DIRECTION ( 'NONE',  ( 0.7071067811865487940, 0.7071067811865463515, 0.000000000000000000 ) ) ;
#133070=CARTESIAN_POINT ( 'NONE',  ( -19.82816939922339117, 21.75929247661550647, 4.000000000000000000 ) ) ;
#133071=LINE ( 'NONE', #101836, #69237 ) ;
#133072=EDGE_LOOP ( 'NONE', ( #107209, #74026, #104137, #3856, #55797 ) ) ;
#133074=CARTESIAN_POINT ( 'NONE',  ( -9.489213562373095101, -27.52281430457062328, 5.000000000000000000 ) ) ;
#133075=AXIS2_PLACEMENT_3D ( 'NONE', #33051, #38721, #14816 ) ;
#133076=DIRECTION ( 'NONE',  ( -1.000000000000000000, 0.000000000000000000, 0.000000000000000000 ) ) ;
#133077=DIRECTION ( 'NONE',  ( 0.7071067811865487940, -0.7071067811865463515, 0.000000000000000000 ) ) ;
#133078=ADVANCED_FACE ( 'NONE', ( #69560 ), #2833, .F. ) ;
#133081=ADVANCED_FACE ( 'NONE', ( #4195 ), #136925, .F. ) ;
#133083=AXIS2_PLACEMENT_3D ( 'NONE', #24412, #4026, #16357 ) ;
#133087=DIRECTION ( 'NONE',  ( 0.7071067811865486830, -0.7071067811865464625, -0.000000000000000000 ) ) ;
#133088=ORIENTED_EDGE ( 'NONE', *, *, #69838, .F. ) ;
#133089=FACE_OUTER_BOUND ( 'NONE', #23050, .T. ) ;
#133090=EDGE_CURVE ( 'NONE', #113958, #102574, #57258, .T. ) ;
#133091=DIRECTION ( 'NONE',  ( -0.000000000000000000, 0.000000000000000000, 1.000000000000000000 ) ) ;
#133092=LINE ( 'NONE', #99705, #120712 ) ;
#133093=CARTESIAN_POINT ( 'NONE',  ( 3.469446951953614189E-15, -1.447814304570820276, 5.000000000000000000 ) ) ;
#133094=DIRECTION ( 'NONE',  ( -0.7071067811865486830, -0.7071067811865464625, 0.000000000000000000 ) ) ;
#133095=CARTESIAN_POINT ( 'NONE',  ( 32.99999999999977263, 13.55218569542903140, 5.000000000000000000 ) ) ;
#133096=VERTEX_POINT ( 'NONE', #113745 ) ;
#133097=DIRECTION ( 'NONE',  ( 0.7071067811865486830, -0.7071067811865464625, -0.000000000000000000 ) ) ;
#133098=CARTESIAN_POINT ( 'NONE',  ( 3.770729005911382714, 22.22500000000000142, 19.66325824265030775 ) ) ;
#133100=ORIENTED_EDGE ( 'NONE', *, *, #62245, .T. ) ;
#133101=AXIS2_PLACEMENT_3D ( 'NONE', #13377, #65700, #112717 ) ;
#133102=VERTEX_POINT ( 'NONE', #101435 ) ;
#133104=VECTOR ( 'NONE', #138146, 1000.000000000000000 ) ;
#133105=ORIENTED_EDGE ( 'NONE', *, *, #77589, .T. ) ;
#133106=AXIS2_PLACEMENT_3D ( 'NONE', #78203, #67330, #60765 ) ;
#133108=CARTESIAN_POINT ( 'NONE',  ( -11.81601139373100651, 28.73617430169779041, 5.000000000000000000 ) ) ;
#133109=CARTESIAN_POINT ( 'NONE',  ( 8.994519915287490619, 28.92564299267944250, 4.000000000000000000 ) ) ;
#133110=CARTESIAN_POINT ( 'NONE',  ( -36.29974487139159578, -27.71228299555231445, 4.000000000000000000 ) ) ;
#133111=FACE_OUTER_BOUND ( 'NONE', #52156, .T. ) ;
#133112=LINE ( 'NONE', #91027, #87210 ) ;
#133113=ORIENTED_EDGE ( 'NONE', *, *, #119514, .T. ) ;
#133115=DIRECTION ( 'NONE',  ( -0.7071067811865486830, -0.7071067811865464625, 0.000000000000000000 ) ) ;
#133116=VERTEX_POINT ( 'NONE', #80429 ) ;
#133117=EDGE_CURVE ( 'NONE', #54672, #105689, #46395, .T. ) ;
#133118=CARTESIAN_POINT ( 'NONE',  ( -0.1839886062690032631, 28.73617430169787568, 5.000000000000000000 ) ) ;
#133119=CARTESIAN_POINT ( 'NONE',  ( -30.18398860626900060, 28.73617430169808173, 5.000000000000000000 ) ) ;
#133120=CARTESIAN_POINT ( 'NONE',  ( 5.510786437626906675, -27.52281430457051314, 5.000000000000000000 ) ) ;
#133121=VERTEX_POINT ( 'NONE', #68843 ) ;
#133122=FACE_BOUND ( 'NONE', #130331, .T. ) ;
#133123=CARTESIAN_POINT ( 'NONE',  ( -32.99999999999976552, 5.587461875839186298, 4.000000000000000000 ) ) ;
#133124=CARTESIAN_POINT ( 'NONE',  ( -60.18398860626900415, 28.73617430169829490, 5.000000000000000000 ) ) ;
#133125=LINE ( 'NONE', #33803, #117687 ) ;
#133131=ORIENTED_EDGE ( 'NONE', *, *, #103718, .F. ) ;
#133134=ADVANCED_FACE ( 'NONE', ( #134820 ), #35516, .T. ) ;
#133135=CARTESIAN_POINT ( 'NONE',  ( 0.000000000000000000, 0.000000000000000000, 5.000000000000000000 ) ) ;
#133136=ORIENTED_EDGE ( 'NONE', *, *, #107541, .F. ) ;
#133137=CARTESIAN_POINT ( 'NONE',  ( -19.05000000000000071, 3.174999999999997158, 4.000000000000000000 ) ) ;
#133139=DIRECTION ( 'NONE',  ( 1.000000000000000000, 0.000000000000000000, 0.000000000000000000 ) ) ;
#133141=VERTEX_POINT ( 'NONE', #36200 ) ;
#133143=DIRECTION ( 'NONE',  ( 0.6830127018922180770, -0.6830127018922204085, -0.2588190451025213501 ) ) ;
#133144=DIRECTION ( 'NONE',  ( 0.3543493200069162685, -0.000000000000000000, -0.9351131265310288487 ) ) ;
#133146=DIRECTION ( 'NONE',  ( 0.7071067811865487940, -0.7071067811865463515, 0.000000000000000000 ) ) ;
#133147=DIRECTION ( 'NONE',  ( 0.3543493200069162685, -0.000000000000000000, -0.9351131265310288487 ) ) ;
#133148=CARTESIAN_POINT ( 'NONE',  ( 9.712309939660210389, -21.73547319004781997, 4.999917730833664642 ) ) ;
#133149=CARTESIAN_POINT ( 'NONE',  ( 24.32816939922335919, -12.74070752338415957, 4.000000000000000000 ) ) ;
#133150=EDGE_LOOP ( 'NONE', ( #54749, #119101, #36433, #120234 ) ) ;
#133151=CARTESIAN_POINT ( 'NONE',  ( -66.48921356237309510, -27.52281430457101763, 5.000000000000000000 ) ) ;
#133152=PLANE ( 'NONE',  #81307 ) ;
#133153=ORIENTED_EDGE ( 'NONE', *, *, #107053, .T. ) ;
#133154=EDGE_LOOP ( 'NONE', ( #137615, #58454, #84549 ) ) ;
#133155=ADVANCED_FACE ( 'NONE', ( #79748 ), #123930, .F. ) ;
#133156=ORIENTED_EDGE ( 'NONE', *, *, #78248, .F. ) ;
#133158=ORIENTED_EDGE ( 'NONE', *, *, #6698, .F. ) ;
#133160=AXIS2_PLACEMENT_3D ( 'NONE', #120921, #132561, #77459 ) ;
#133165=VERTEX_POINT ( 'NONE', #57979 ) ;
#133167=CARTESIAN_POINT ( 'NONE',  ( -2.994519915287485734, 28.92564299267940342, 4.000000000000000000 ) ) ;
#133168=VERTEX_POINT ( 'NONE', #102175 ) ;
#133169=CARTESIAN_POINT ( 'NONE',  ( -2.671830600776449405, 8.259292476615637923, 4.000000000000000000 ) ) ;
#133170=DIRECTION ( 'NONE',  ( 0.7071067811865486830, -0.7071067811865464625, -0.000000000000000000 ) ) ;
#133171=ORIENTED_EDGE ( 'NONE', *, *, #13405, .T. ) ;
#133172=DIRECTION ( 'NONE',  ( -0.000000000000000000, 0.000000000000000000, 1.000000000000000000 ) ) ;
#133173=VECTOR ( 'NONE', #62249, 1000.000000000000114 ) ;
#133175=EDGE_LOOP ( 'NONE', ( #12839, #89942, #9824, #76574 ) ) ;
#133176=ORIENTED_EDGE ( 'NONE', *, *, #79896, .T. ) ;
#133178=EDGE_CURVE ( 'NONE', #88227, #19705, #91311, .T. ) ;
#133179=DIRECTION ( 'NONE',  ( -0.7071067811865486830, 0.7071067811865464625, 0.000000000000000000 ) ) ;
#133182=ADVANCED_FACE ( 'NONE', ( #41172 ), #29574, .T. ) ;
#133183=ORIENTED_EDGE ( 'NONE', *, *, #50733, .F. ) ;
#133184=DIRECTION ( 'NONE',  ( -0.3543493200069162685, -0.000000000000000000, -0.9351131265310288487 ) ) ;
#133186=VECTOR ( 'NONE', #41218, 1000.000000000000000 ) ;
#133187=EDGE_CURVE ( 'NONE', #10027, #66379, #18687, .T. ) ;
#133188=EDGE_CURVE ( 'NONE', #73197, #98076, #107141, .T. ) ;
#133189=VECTOR ( 'NONE', #135829, 999.9999999999998863 ) ;
#133191=CARTESIAN_POINT ( 'NONE',  ( -3.707013264293017141, -21.74070752338405299, 4.999753212805222446 ) ) ;
#133193=EDGE_CURVE ( 'NONE', #86287, #49673, #71682, .T. ) ;
#133194=DIRECTION ( 'NONE',  ( 0.3543493200069162685, -0.000000000000000000, -0.9351131265310288487 ) ) ;
#133195=VECTOR ( 'NONE', #8615, 1000.000000000000227 ) ;
#133196=DIRECTION ( 'NONE',  ( -0.000000000000000000, -0.3543493200069152693, 0.9351131265310292928 ) ) ;
#133197=ORIENTED_EDGE ( 'NONE', *, *, #1401, .T. ) ;
#133198=ORIENTED_EDGE ( 'NONE', *, *, #93888, .F. ) ;
#133200=ORIENTED_EDGE ( 'NONE', *, *, #128837, .T. ) ;
#133201=DIRECTION ( 'NONE',  ( 0.7071067811865487940, -0.7071067811865463515, 0.000000000000000000 ) ) ;
#133204=DIRECTION ( 'NONE',  ( -1.000000000000000000, 0.000000000000000000, -0.000000000000000000 ) ) ;
#133205=CARTESIAN_POINT ( 'NONE',  ( -34.92500000000001137, 22.22500000000000142, 4.000000000000000000 ) ) ;
#133206=ADVANCED_FACE ( 'NONE', ( #84011 ), #85381, .F. ) ;
#133207=CARTESIAN_POINT ( 'NONE',  ( -24.32816939922335209, 11.25929247661560950, 4.000000000000000000 ) ) ;
#133209=DIRECTION ( 'NONE',  ( 0.7071067811865486830, -0.7071067811865464625, -0.000000000000000000 ) ) ;
#133211=ORIENTED_EDGE ( 'NONE', *, *, #6457, .F. ) ;
#133213=VERTEX_POINT ( 'NONE', #128892 ) ;
#133215=ORIENTED_EDGE ( 'NONE', *, *, #42703, .T. ) ;
#133216=EDGE_CURVE ( 'NONE', #62934, #101394, #26732, .T. ) ;
#133217=DIRECTION ( 'NONE',  ( -0.6830127018922181881, 0.6830127018922202975, -0.2588190451025214056 ) ) ;
#133218=CARTESIAN_POINT ( 'NONE',  ( 5.999999999999964473, 19.93112307739198386, 4.000000000000000000 ) ) ;
#133221=CARTESIAN_POINT ( 'NONE',  ( 0.000000000000000000, 0.000000000000000000, 5.000000000000000000 ) ) ;
#133222=ORIENTED_EDGE ( 'NONE', *, *, #133216, .T. ) ;
#133224=ORIENTED_EDGE ( 'NONE', *, *, #40773, .F. ) ;
#133226=ORIENTED_EDGE ( 'NONE', *, *, #95104, .T. ) ;
#133227=EDGE_CURVE ( 'NONE', #98041, #1156, #70975, .T. ) ;
#133228=CARTESIAN_POINT ( 'NONE',  ( 0.000000000000000000, 0.000000000000000000, 5.000000000000000000 ) ) ;
#133231=FACE_OUTER_BOUND ( 'NONE', #117462, .T. ) ;
#133234=CARTESIAN_POINT ( 'NONE',  ( -23.20710678118637915, -8.240707523384202204, 5.000000000000000000 ) ) ;
#133237=CARTESIAN_POINT ( 'NONE',  ( 2.994519915287485734, 28.92564299267940342, 4.000000000000000000 ) ) ;
#133238=PLANE ( 'NONE',  #23469 ) ;
#133239=DIRECTION ( 'NONE',  ( -0.7071067811865486830, -0.7071067811865464625, 0.000000000000000000 ) ) ;
#133241=ORIENTED_EDGE ( 'NONE', *, *, #59534, .T. ) ;
#133243=ORIENTED_EDGE ( 'NONE', *, *, #106707, .F. ) ;
#133245=EDGE_CURVE ( 'NONE', #74481, #38431, #60098, .T. ) ;
#133246=LINE ( 'NONE', #112891, #108134 ) ;
#133247=CARTESIAN_POINT ( 'NONE',  ( 10.49999999999993250, 3.052185695429136647, 5.000000000000000000 ) ) ;
#133248=DIRECTION ( 'NONE',  ( -0.7071067811865486830, -0.7071067811865464625, 0.000000000000000000 ) ) ;
#133249=FACE_OUTER_BOUND ( 'NONE', #76907, .T. ) ;
#133250=ORIENTED_EDGE ( 'NONE', *, *, #73362, .F. ) ;
#133251=CARTESIAN_POINT ( 'NONE',  ( 11.99999999999991296, 19.93112307739198386, 4.000000000000000000 ) ) ;
#133253=EDGE_CURVE ( 'NONE', #89658, #59700, #139080, .T. ) ;
#133254=CARTESIAN_POINT ( 'NONE',  ( -17.28242261357420873, -21.73023691814492864, 5.000000000000000000 ) ) ;
#133256=DIRECTION ( 'NONE',  ( -0.000000000000000000, 0.3543493200069153248, 0.9351131265310292928 ) ) ;
#133257=CARTESIAN_POINT ( 'NONE',  ( 23.67183060077630685, -12.74070752338415069, 4.000000000000000000 ) ) ;
#133258=ORIENTED_EDGE ( 'NONE', *, *, #78541, .T. ) ;
#133259=LINE ( 'NONE', #57140, #10612 ) ;
#133261=LINE ( 'NONE', #80314, #34050 ) ;
#133262=EDGE_CURVE ( 'NONE', #58070, #88273, #111915, .T. ) ;
#133263=LINE ( 'NONE', #88324, #111651 ) ;
#133264=VERTEX_POINT ( 'NONE', #28170 ) ;
#133265=ORIENTED_EDGE ( 'NONE', *, *, #50871, .F. ) ;
#133266=VERTEX_POINT ( 'NONE', #16551 ) ;
#133268=ORIENTED_EDGE ( 'NONE', *, *, #8714, .F. ) ;
#133270=ADVANCED_FACE ( 'NONE', ( #94116 ), #39038, .F. ) ;
#133272=LINE ( 'NONE', #54991, #20174 ) ;
#133273=CARTESIAN_POINT ( 'NONE',  ( -32.99999999999976552, -13.44781430457069149, 5.000000000000000000 ) ) ;
#133274=DIRECTION ( 'NONE',  ( 0.7071067811865486830, -0.7071067811865464625, -0.000000000000000000 ) ) ;
#133275=ORIENTED_EDGE ( 'NONE', *, *, #3543, .F. ) ;
#133276=LINE ( 'NONE', #78173, #53740 ) ;
#133277=LINE ( 'NONE', #90467, #88347 ) ;
#133279=VECTOR ( 'NONE', #127313, 1000.000000000000000 ) ;
#133280=ORIENTED_EDGE ( 'NONE', *, *, #112693, .F. ) ;
#133281=EDGE_CURVE ( 'NONE', #4087, #27739, #116598, .T. ) ;
#133282=CARTESIAN_POINT ( 'NONE',  ( 26.29289321881327623, 11.25929247661560773, 5.000000000000000000 ) ) ;
#133283=LINE ( 'NONE', #98485, #42367 ) ;
#133285=ORIENTED_EDGE ( 'NONE', *, *, #93534, .F. ) ;
#133286=EDGE_CURVE ( 'NONE', #142768, #13302, #6353, .T. ) ;
#133287=CARTESIAN_POINT ( 'NONE',  ( -34.49999999999975842, 16.77039438581775954, 0.4657186855308521056 ) ) ;
#133288=ADVANCED_FACE ( 'NONE', ( #28885 ), #17960, .F. ) ;
#133290=DIRECTION ( 'NONE',  ( 0.7071067811865487940, 0.7071067811865463515, -0.000000000000000000 ) ) ;
#133291=CARTESIAN_POINT ( 'NONE',  ( -28.49999999999979039, 3.052185695429140200, 5.000000000000000000 ) ) ;
#133292=VECTOR ( 'NONE', #33084, 1000.000000000000227 ) ;
#133293=PLANE ( 'NONE',  #97318 ) ;
#133294=PLANE ( 'NONE',  #96007 ) ;
#133295=EDGE_CURVE ( 'NONE', #92540, #92320, #141192, .T. ) ;
#133296=VECTOR ( 'NONE', #135229, 1000.000000000000000 ) ;
#133298=VECTOR ( 'NONE', #93578, 1000.000000000000000 ) ;
#133299=VERTEX_POINT ( 'NONE', #54238 ) ;
#133300=EDGE_LOOP ( 'NONE', ( #129656, #93338, #139389, #69829 ) ) ;
#133301=ORIENTED_EDGE ( 'NONE', *, *, #108060, .F. ) ;
#133303=EDGE_CURVE ( 'NONE', #129197, #17080, #20119, .T. ) ;
#133304=DIRECTION ( 'NONE',  ( -0.7071067811865486830, 0.7071067811865464625, 0.000000000000000000 ) ) ;
#133305=EDGE_CURVE ( 'NONE', #86591, #74065, #9213, .T. ) ;
#133306=ORIENTED_EDGE ( 'NONE', *, *, #59010, .F. ) ;
#133309=PLANE ( 'NONE',  #64212 ) ;
#133310=CARTESIAN_POINT ( 'NONE',  ( 34.92499999999998295, 22.22500000000000142, 4.500000000000000888 ) ) ;
#133312=ORIENTED_EDGE ( 'NONE', *, *, #57435, .T. ) ;
#133314=VERTEX_POINT ( 'NONE', #99843 ) ;
#133315=DIRECTION ( 'NONE',  ( -0.3543493200069163240, 4.681814790819596721E-17, -0.9351131265310288487 ) ) ;
#133317=CARTESIAN_POINT ( 'NONE',  ( -44.99451991528749772, 28.92564299267969474, 4.000000000000000000 ) ) ;
#133319=VERTEX_POINT ( 'NONE', #66516 ) ;
#133320=DIRECTION ( 'NONE',  ( 0.7071067811865486830, -0.7071067811865464625, -0.000000000000000000 ) ) ;
#133321=EDGE_LOOP ( 'NONE', ( #92498, #141456, #14865, #57292 ) ) ;
#133323=EDGE_LOOP ( 'NONE', ( #10637, #115032, #98559, #90039 ) ) ;
#133324=CARTESIAN_POINT ( 'NONE',  ( 66.29974487139159578, -27.71228299555252406, 4.000000000000000000 ) ) ;
#133326=LINE ( 'NONE', #142755, #79725 ) ;
#133328=DIRECTION ( 'NONE',  ( 0.7071067811865487940, -0.7071067811865463515, 0.000000000000000000 ) ) ;
#133329=DIRECTION ( 'NONE',  ( -0.3543493200069162685, -0.000000000000000000, -0.9351131265310288487 ) ) ;
#133332=ORIENTED_EDGE ( 'NONE', *, *, #111004, .F. ) ;
#133333=LINE ( 'NONE', #36163, #39091 ) ;
#133334=DIRECTION ( 'NONE',  ( 0.7071067811865487940, 0.7071067811865463515, -0.000000000000000000 ) ) ;
#133335=EDGE_LOOP ( 'NONE', ( #97174, #108870, #26141, #79560 ) ) ;
#133336=ORIENTED_EDGE ( 'NONE', *, *, #88541, .F. ) ;
#133337=EDGE_CURVE ( 'NONE', #135646, #133878, #33205, .T. ) ;
#133339=CARTESIAN_POINT ( 'NONE',  ( 42.18398860626899705, 28.73617430169816700, 5.000000000000000000 ) ) ;
#133340=VERTEX_POINT ( 'NONE', #109996 ) ;
#133341=VERTEX_POINT ( 'NONE', #74546 ) ;
#133342=CARTESIAN_POINT ( 'NONE',  ( -23.99451991528749062, 28.92564299267954908, 4.000000000000000000 ) ) ;
#133344=CARTESIAN_POINT ( 'NONE',  ( 28.55334942336764925, 2.259292476615690770, 14.86850063742347849 ) ) ;
#133345=CARTESIAN_POINT ( 'NONE',  ( -8.292893218813400580, -6.740707523384218192, 5.000000000000000000 ) ) ;
#133346=ORIENTED_EDGE ( 'NONE', *, *, #38911, .F. ) ;
#133347=CARTESIAN_POINT ( 'NONE',  ( -50.99451991528749062, 28.92564299267973738, 4.000000000000000000 ) ) ;
#133348=ORIENTED_EDGE ( 'NONE', *, *, #96638, .F. ) ;
#133349=DIRECTION ( 'NONE',  ( 0.7071067811865486830, -0.7071067811865464625, -0.000000000000000000 ) ) ;
#133350=AXIS2_PLACEMENT_3D ( 'NONE', #132425, #141853, #85284 ) ;
#133351=ADVANCED_FACE ( 'NONE', ( #108535 ), #22252, .F. ) ;
#133356=PLANE ( 'NONE',  #96775 ) ;
#133358=DIRECTION ( 'NONE',  ( -0.7071067811865487940, 0.7071067811865463515, -0.000000000000000000 ) ) ;
#133359=VERTEX_POINT ( 'NONE', #30303 ) ;
#133360=ORIENTED_EDGE ( 'NONE', *, *, #88034, .T. ) ;
#133361=EDGE_CURVE ( 'NONE', #39023, #116419, #61468, .T. ) ;
#133362=ORIENTED_EDGE ( 'NONE', *, *, #107788, .T. ) ;
#133363=CARTESIAN_POINT ( 'NONE',  ( 19.05000000000000071, 3.174999999999997158, 4.000000000000000000 ) ) ;
#133364=FACE_OUTER_BOUND ( 'NONE', #51420, .T. ) ;
#133365=CARTESIAN_POINT ( 'NONE',  ( -8.816011393731004731, 28.73617430169781173, 5.000000000000000000 ) ) ;
#133366=CARTESIAN_POINT ( 'NONE',  ( 10.49999999999992539, -15.29013452822853125, 0.3645803511610583580 ) ) ;
#133367=ADVANCED_FACE ( 'NONE', ( #141953 ), #87543, .F. ) ;
#133368=PLANE ( 'NONE',  #54231 ) ;
#133369=EDGE_LOOP ( 'NONE', ( #126751, #53893, #82153 ) ) ;
#133370=LINE ( 'NONE', #11536, #112916 ) ;
#133371=VECTOR ( 'NONE', #13065, 1000.000000000000000 ) ;
#133373=LINE ( 'NONE', #79744, #23430 ) ;
#133375=ORIENTED_EDGE ( 'NONE', *, *, #139142, .T. ) ;
#133376=DIRECTION ( 'NONE',  ( -0.6830127018922181881, 0.6830127018922202975, -0.2588190451025214056 ) ) ;
#133377=CARTESIAN_POINT ( 'NONE',  ( -56.99451991528749062, 28.92564299267978001, 4.000000000000000000 ) ) ;
#133378=ORIENTED_EDGE ( 'NONE', *, *, #53574, .F. ) ;
#133379=ADVANCED_FACE ( 'NONE', ( #99098 ), #31735, .F. ) ;
#133380=CARTESIAN_POINT ( 'NONE',  ( 26.99999999999980105, -16.02097659208070368, -11.96015758381215477 ) ) ;
#133381=ORIENTED_EDGE ( 'NONE', *, *, #121780, .F. ) ;
#133382=ORIENTED_EDGE ( 'NONE', *, *, #131913, .T. ) ;
#133383=EDGE_CURVE ( 'NONE', #67347, #21681, #120128, .T. ) ;
#133384=DIRECTION ( 'NONE',  ( 0.6830127018922181881, 0.6830127018922202975, -0.2588190451025214056 ) ) ;
#133385=CARTESIAN_POINT ( 'NONE',  ( -0.7928932188134494297, 3.759292476615678336, 5.000000000000000000 ) ) ;
#133386=ORIENTED_EDGE ( 'NONE', *, *, #38912, .F. ) ;
#133387=PLANE ( 'NONE',  #67553 ) ;
#133389=EDGE_CURVE ( 'NONE', #70502, #91018, #109289, .T. ) ;
#133390=FACE_OUTER_BOUND ( 'NONE', #28894, .T. ) ;
#133391=VECTOR ( 'NONE', #67674, 1000.000000000000000 ) ;
#133392=DIRECTION ( 'NONE',  ( -0.000000000000000000, 0.000000000000000000, 1.000000000000000000 ) ) ;
#133393=DIRECTION ( 'NONE',  ( -0.7071067811865486830, -0.7071067811865464625, -0.000000000000000000 ) ) ;
#133394=CARTESIAN_POINT ( 'NONE',  ( 57.18398860626899705, 28.73617430169827358, 5.000000000000000000 ) ) ;
#133395=VECTOR ( 'NONE', #45721, 1000.000000000000000 ) ;
#133396=FACE_OUTER_BOUND ( 'NONE', #80461, .T. ) ;
#133397=LINE ( 'NONE', #97901, #95782 ) ;
#133400=DIRECTION ( 'NONE',  ( 0.3543493200069162685, -0.000000000000000000, -0.9351131265310288487 ) ) ;
#133401=FACE_OUTER_BOUND ( 'NONE', #21705, .T. ) ;
#133402=AXIS2_PLACEMENT_3D ( 'NONE', #58184, #69763, #103749 ) ;
#133403=PLANE ( 'NONE',  #53493 ) ;
#133404=LINE ( 'NONE', #54429, #112588 ) ;
#133405=ORIENTED_EDGE ( 'NONE', *, *, #131759, .T. ) ;
#133408=VERTEX_POINT ( 'NONE', #9972 ) ;
#133409=ORIENTED_EDGE ( 'NONE', *, *, #116529, .F. ) ;
#133410=EDGE_LOOP ( 'NONE', ( #5389, #82668, #56276, #126472 ) ) ;
#133413=PLANE ( 'NONE',  #118113 ) ;
#133414=ORIENTED_EDGE ( 'NONE', *, *, #103934, .F. ) ;
#133416=CARTESIAN_POINT ( 'NONE',  ( -4.499999999999968914, -12.66682484999667047, -0.6294897503864036459 ) ) ;
#133417=CARTESIAN_POINT ( 'NONE',  ( 28.96659967656959722, 6.759292476615649470, 12.28218704918528736 ) ) ;
#133419=ORIENTED_EDGE ( 'NONE', *, *, #63952, .F. ) ;
#133420=FACE_OUTER_BOUND ( 'NONE', #133954, .T. ) ;
#133423=LINE ( 'NONE', #12331, #54540 ) ;
#133424=CARTESIAN_POINT ( 'NONE',  ( 23.70025512860841133, -27.71228299555189523, 4.000000000000000000 ) ) ;
#133426=DIRECTION ( 'NONE',  ( -0.7071067811865486830, -0.7071067811865464625, 0.000000000000000000 ) ) ;
#133427=EDGE_CURVE ( 'NONE', #129470, #42524, #32459, .T. ) ;
#133429=ORIENTED_EDGE ( 'NONE', *, *, #142582, .T. ) ;
#133432=ORIENTED_EDGE ( 'NONE', *, *, #81364, .F. ) ;
#133433=EDGE_CURVE ( 'NONE', #124008, #24896, #58544, .T. ) ;
#133434=DIRECTION ( 'NONE',  ( 0.000000000000000000, 0.000000000000000000, -1.000000000000000000 ) ) ;
#133435=AXIS2_PLACEMENT_3D ( 'NONE', #22130, #66384, #55510 ) ;
#133436=DIRECTION ( 'NONE',  ( 0.7071067811865487940, 0.7071067811865463515, 0.000000000000000000 ) ) ;
#133437=DIRECTION ( 'NONE',  ( -0.7071067811865486830, -0.7071067811865464625, -0.000000000000000000 ) ) ;
#133438=CARTESIAN_POINT ( 'NONE',  ( 3.328169399223508851, -12.74070752338415247, 4.000000000000000000 ) ) ;
#133440=ORIENTED_EDGE ( 'NONE', *, *, #9139, .T. ) ;
#133442=ORIENTED_EDGE ( 'NONE', *, *, #60958, .F. ) ;
#133445=PLANE ( 'NONE',  #33949 ) ;
#133446=( BOUNDED_CURVE ( )  B_SPLINE_CURVE ( 3, ( #52270, #141428, #96455, #118951 ),
 .UNSPECIFIED., .F., .T. ) 
 B_SPLINE_CURVE_WITH_KNOTS ( ( 4, 4 ),
 ( 4.874499669516390910, 4.920172610314182293 ),
 .UNSPECIFIED. ) 
 CURVE ( )  GEOMETRIC_REPRESENTATION_ITEM ( )  RATIONAL_B_SPLINE_CURVE ( ( 1.000000000000000000, 0.9998261727610758820, 0.9998261727610758820, 1.000000000000000000 ) ) 
 REPRESENTATION_ITEM ( '' )  );
#133447=ORIENTED_EDGE ( 'NONE', *, *, #96086, .F. ) ;
#133448=VERTEX_POINT ( 'NONE', #59928 ) ;
#133450=EDGE_CURVE ( 'NONE', #14639, #54134, #138917, .T. ) ;
#133451=VERTEX_POINT ( 'NONE', #92515 ) ;
#133454=CARTESIAN_POINT ( 'NONE',  ( 15.48921356237309510, -27.52281430457066236, 5.000000000000000000 ) ) ;
#133455=AXIS2_PLACEMENT_3D ( 'NONE', #1830, #46133, #134566 ) ;
#133457=ORIENTED_EDGE ( 'NONE', *, *, #9325, .F. ) ;
#133459=VERTEX_POINT ( 'NONE', #128049 ) ;
#133460=ORIENTED_EDGE ( 'NONE', *, *, #138082, .T. ) ;
#133464=EDGE_CURVE ( 'NONE', #102488, #17773, #71512, .T. ) ;
#133465=ORIENTED_EDGE ( 'NONE', *, *, #15132, .T. ) ;
#133466=LINE ( 'NONE', #56661, #110756 ) ;
#133467=VECTOR ( 'NONE', #32381, 1000.000000000000000 ) ;
#133468=DIRECTION ( 'NONE',  ( 1.000000000000000000, 0.000000000000000000, 0.000000000000000000 ) ) ;
#133470=EDGE_CURVE ( 'NONE', #123427, #97084, #49054, .T. ) ;
#133471=VECTOR ( 'NONE', #25736, 999.9999999999998863 ) ;
#133472=FACE_BOUND ( 'NONE', #130867, .T. ) ;
#133473=VERTEX_POINT ( 'NONE', #115674 ) ;
#133474=PLANE ( 'NONE',  #87408 ) ;
#133475=FACE_OUTER_BOUND ( 'NONE', #4734, .T. ) ;
#133476=CARTESIAN_POINT ( 'NONE',  ( 21.48921356237309155, -27.52281430457070499, 5.000000000000000000 ) ) ;
#133477=CARTESIAN_POINT ( 'NONE',  ( 18.00548008471250583, 28.92564299267925776, 4.000000000000000000 ) ) ;
#133478=ADVANCED_FACE ( 'NONE', ( #128734 ), #17806, .F. ) ;
#133479=ORIENTED_EDGE ( 'NONE', *, *, #113073, .T. ) ;
#133480=PLANE ( 'NONE',  #142984 ) ;
#133481=VERTEX_POINT ( 'NONE', #28002 ) ;
#133482=EDGE_LOOP ( 'NONE', ( #36610, #139794, #11115, #40314 ) ) ;
#133483=VECTOR ( 'NONE', #6609, 1000.000000000000000 ) ;
#133484=ORIENTED_EDGE ( 'NONE', *, *, #55288, .F. ) ;
#133485=VECTOR ( 'NONE', #55362, 1000.000000000000000 ) ;
#133486=VECTOR ( 'NONE', #36271, 1000.000000000000227 ) ;
#133488=ORIENTED_EDGE ( 'NONE', *, *, #124996, .T. ) ;
#133489=FACE_OUTER_BOUND ( 'NONE', #85324, .T. ) ;
#133491=VERTEX_POINT ( 'NONE', #38875 ) ;
#133492=CARTESIAN_POINT ( 'NONE',  ( -15.00548008471250228, 28.92564299267927552, 4.000000000000000000 ) ) ;
#133493=AXIS2_PLACEMENT_3D ( 'NONE', #78855, #24446, #36065 ) ;
#133494=EDGE_CURVE ( 'NONE', #55424, #126070, #127299, .T. ) ;
#133495=DIRECTION ( 'NONE',  ( -0.7071067811865487940, 0.7071067811865463515, -0.000000000000000000 ) ) ;
#133496=DIRECTION ( 'NONE',  ( -0.6830127018922181881, 0.6830127018922202975, -0.2588190451025214056 ) ) ;
#133497=DIRECTION ( 'NONE',  ( -1.000000000000000000, 0.000000000000000000, -0.000000000000000000 ) ) ;
#133498=CARTESIAN_POINT ( 'NONE',  ( -6.707106781186485733, -12.74070752338415602, 5.000000000000000000 ) ) ;
#133499=DIRECTION ( 'NONE',  ( 0.7071067811865486830, -0.7071067811865464625, -0.000000000000000000 ) ) ;
#133501=ORIENTED_EDGE ( 'NONE', *, *, #116652, .F. ) ;
#133502=ORIENTED_EDGE ( 'NONE', *, *, #4660, .F. ) ;
#133503=ORIENTED_EDGE ( 'NONE', *, *, #101625, .T. ) ;
#133504=LINE ( 'NONE', #134221, #42716 ) ;
#133505=LINE ( 'NONE', #76271, #51387 ) ;
#133506=VERTEX_POINT ( 'NONE', #50473 ) ;
#133507=ORIENTED_EDGE ( 'NONE', *, *, #90558, .F. ) ;
#133508=CARTESIAN_POINT ( 'NONE',  ( -14.99999999999988454, -10.44781430457071814, 5.000000000000000000 ) ) ;
#133509=DIRECTION ( 'NONE',  ( -0.7071067811865486830, 0.7071067811865464625, 0.000000000000000000 ) ) ;
#133511=ORIENTED_EDGE ( 'NONE', *, *, #106476, .F. ) ;
#133512=LINE ( 'NONE', #34200, #48670 ) ;
#133513=DIRECTION ( 'NONE',  ( -0.000000000000000000, 0.3543493200069153248, 0.9351131265310292928 ) ) ;
#133515=EDGE_CURVE ( 'NONE', #123567, #141805, #6196, .T. ) ;
#133516=VECTOR ( 'NONE', #23099, 1000.000000000000000 ) ;
#133517=LINE ( 'NONE', #89, #64366 ) ;
#133518=EDGE_LOOP ( 'NONE', ( #129834, #47354, #110941, #70282 ) ) ;
#133520=ADVANCED_FACE ( 'NONE', ( #51192 ), #93959, .F. ) ;
#133521=DIRECTION ( 'NONE',  ( 1.000000000000000000, 0.000000000000000000, 0.000000000000000000 ) ) ;
#133522=CARTESIAN_POINT ( 'NONE',  ( -15.18398860626900237, 28.73617430169797871, 5.000000000000000000 ) ) ;
#133523=DIRECTION ( 'NONE',  ( 0.3543493200069164351, 2.781805975412904658E-17, -0.9351131265310288487 ) ) ;
#133524=LINE ( 'NONE', #77722, #75021 ) ;
#133525=ORIENTED_EDGE ( 'NONE', *, *, #46240, .T. ) ;
#133526=VECTOR ( 'NONE', #47875, 999.9999999999998863 ) ;
#133527=PLANE ( 'NONE',  #64854 ) ;
#133528=VERTEX_POINT ( 'NONE', #106235 ) ;
#133529=DIRECTION ( 'NONE',  ( -0.3543493200069162685, -0.000000000000000000, -0.9351131265310288487 ) ) ;
#133530=DIRECTION ( 'NONE',  ( 0.3543493200069162685, -0.000000000000000000, -0.9351131265310288487 ) ) ;
#133531=ADVANCED_FACE ( 'NONE', ( #48319 ), #117824, .F. ) ;
#133532=EDGE_CURVE ( 'NONE', #32577, #30830, #73649, .T. ) ;
#133534=ORIENTED_EDGE ( 'NONE', *, *, #82592, .F. ) ;
#133536=LINE ( 'NONE', #90003, #23312 ) ;
#133537=CARTESIAN_POINT ( 'NONE',  ( -14.99451991528749595, 28.92564299267948513, 4.000000000000000000 ) ) ;
#133538=VECTOR ( 'NONE', #45866, 1000.000000000000227 ) ;
#133540=CARTESIAN_POINT ( 'NONE',  ( -4.499999999999968914, 0.4497235411627387158, -5.599840258123551351 ) ) ;
#133543=CARTESIAN_POINT ( 'NONE',  ( 34.49999999999975131, 16.18958161055405753, -11.56426086740803427 ) ) ;
#133544=VECTOR ( 'NONE', #54494, 1000.000000000000227 ) ;
#133546=EDGE_LOOP ( 'NONE', ( #111275, #95077, #25762, #45471, #77512, #35455 ) ) ;
#133547=ADVANCED_FACE ( 'NONE', ( #106974 ), #26570, .F. ) ;
#133548=ORIENTED_EDGE ( 'NONE', *, *, #121299, .F. ) ;
#133549=DIRECTION ( 'NONE',  ( 0.7071067811865487940, 0.7071067811865463515, -0.000000000000000000 ) ) ;
#133550=CARTESIAN_POINT ( 'NONE',  ( 31.49999999999977973, -13.91253812416061386, 4.000000000000000000 ) ) ;
#133551=ORIENTED_EDGE ( 'NONE', *, *, #130, .F. ) ;
#133552=EDGE_CURVE ( 'NONE', #67920, #86102, #125897, .T. ) ;
#133553=VECTOR ( 'NONE', #121868, 1000.000000000000000 ) ;
#133554=DIRECTION ( 'NONE',  ( -0.7071067811865487940, 0.7071067811865463515, -0.000000000000000000 ) ) ;
#133555=LINE ( 'NONE', #25475, #4340 ) ;
#133558=ORIENTED_EDGE ( 'NONE', *, *, #80871, .F. ) ;
#133559=DIRECTION ( 'NONE',  ( 0.7071067811865487940, -0.7071067811865463515, 0.000000000000000000 ) ) ;
#133560=DIRECTION ( 'NONE',  ( -0.7071067811865486830, -0.7071067811865464625, 0.000000000000000000 ) ) ;
#133561=VECTOR ( 'NONE', #32862, 1000.000000000000000 ) ;
#133562=CARTESIAN_POINT ( 'NONE',  ( 1.499999999999997780, 7.087461875839172087, 4.000000000000000000 ) ) ;
#133567=ORIENTED_EDGE ( 'NONE', *, *, #116128, .F. ) ;
#133568=ORIENTED_EDGE ( 'NONE', *, *, #122719, .T. ) ;
#133569=CARTESIAN_POINT ( 'NONE',  ( -38.99451991528749062, 28.92564299267965211, 4.000000000000000000 ) ) ;
#133570=ORIENTED_EDGE ( 'NONE', *, *, #55162, .F. ) ;
#133571=VERTEX_POINT ( 'NONE', #97524 ) ;
#133572=ORIENTED_EDGE ( 'NONE', *, *, #41427, .F. ) ;
#133573=ADVANCED_FACE ( 'NONE', ( #22100 ), #31576, .T. ) ;
#133574=PLANE ( 'NONE',  #128970 ) ;
#133575=DIRECTION ( 'NONE',  ( -0.7071067811865487940, 0.7071067811865463515, -0.000000000000000000 ) ) ;
#133576=ORIENTED_EDGE ( 'NONE', *, *, #75218, .T. ) ;
#133577=CARTESIAN_POINT ( 'NONE',  ( -21.29974487139158512, -27.71228299555221142, 4.000000000000000000 ) ) ;
#133578=CARTESIAN_POINT ( 'NONE',  ( 28.49999999999980105, 8.900465351122175406, -2.516491619111579592 ) ) ;
#133579=LINE ( 'NONE', #883, #69475 ) ;
#133580=VECTOR ( 'NONE', #64439, 1000.000000000000227 ) ;
#133581=CARTESIAN_POINT ( 'NONE',  ( 39.18398860626899705, 28.73617430169814568, 5.000000000000000000 ) ) ;
#133583=VERTEX_POINT ( 'NONE', #54766 ) ;
#133584=EDGE_CURVE ( 'NONE', #56805, #104812, #109839, .T. ) ;
#133585=CARTESIAN_POINT ( 'NONE',  ( -22.64175702458846828, 15.75929247661555088, 19.34181609438704541 ) ) ;
#133586=CARTESIAN_POINT ( 'NONE',  ( -57.18398860626899705, 28.73617430169827358, 5.000000000000000000 ) ) ;
#133587=CARTESIAN_POINT ( 'NONE',  ( -11.27718569542934191, -21.72500000000000853, 5.000000000000000000 ) ) ;
#133588=CARTESIAN_POINT ( 'NONE',  ( -13.49999999999990763, -1.533600742197719580, 5.000000000000000000 ) ) ;
#133589=PLANE ( 'NONE',  #31222 ) ;
#133590=VECTOR ( 'NONE', #118460, 1000.000000000000000 ) ;
#133595=EDGE_CURVE ( 'NONE', #91203, #50701, #64206, .T. ) ;
#133596=FACE_OUTER_BOUND ( 'NONE', #31068, .T. ) ;
#133597=VECTOR ( 'NONE', #9645, 1000.000000000000000 ) ;
#133598=LINE ( 'NONE', #45887, #39215 ) ;
#133599=EDGE_LOOP ( 'NONE', ( #65176, #54682, #141957, #3612 ) ) ;
#133600=VERTEX_POINT ( 'NONE', #98262 ) ;
#133603=VECTOR ( 'NONE', #19475, 1000.000000000000000 ) ;
#133605=CARTESIAN_POINT ( 'NONE',  ( 45.48921356237309510, -27.52281430457087197, 5.000000000000000000 ) ) ;
#133606=ORIENTED_EDGE ( 'NONE', *, *, #39422, .T. ) ;
#133607=DIRECTION ( 'NONE',  ( 0.6830127018922180770, -0.6830127018922202975, -0.2588190451025213501 ) ) ;
#133608=LINE ( 'NONE', #37131, #127979 ) ;
#133610=ORIENTED_EDGE ( 'NONE', *, *, #126365, .T. ) ;
#133611=CARTESIAN_POINT ( 'NONE',  ( -34.47516574401890210, -4.509482387884336418, 4.998110765256836174 ) ) ;
#133612=EDGE_LOOP ( 'NONE', ( #24386, #115324, #17099, #29120 ) ) ;
#133613=ORIENTED_EDGE ( 'NONE', *, *, #13037, .F. ) ;
#133614=CARTESIAN_POINT ( 'NONE',  ( -39.18398860626899705, 28.73617430169814568, 5.000000000000000000 ) ) ;
#133615=LINE ( 'NONE', #34290, #38389 ) ;
#133616=CARTESIAN_POINT ( 'NONE',  ( -42.29974487139158157, -27.71228299555235708, 4.000000000000000000 ) ) ;
#133617=ORIENTED_EDGE ( 'NONE', *, *, #99935, .T. ) ;
#133618=DIRECTION ( 'NONE',  ( -0.000000000000000000, -0.000000000000000000, 1.000000000000000000 ) ) ;
#133620=CARTESIAN_POINT ( 'NONE',  ( -42.18398860626899705, 28.73617430169816700, 5.000000000000000000 ) ) ;
#133621=LINE ( 'NONE', #90847, #18373 ) ;
#133622=CARTESIAN_POINT ( 'NONE',  ( -39.48921356237310221, -27.52281430457082934, 5.000000000000000000 ) ) ;
#133624=VECTOR ( 'NONE', #1170, 1000.000000000000227 ) ;
#133625=LINE ( 'NONE', #138434, #25389 ) ;
#133626=( BOUNDED_CURVE ( )  B_SPLINE_CURVE ( 3, ( #118385, #55303, #53892, #86506 ),
 .UNSPECIFIED., .F., .T. ) 
 B_SPLINE_CURVE_WITH_KNOTS ( ( 4, 4 ),
 ( 5.043186909253423167, 5.074607125596354074 ),
 .UNSPECIFIED. ) 
 CURVE ( )  GEOMETRIC_REPRESENTATION_ITEM ( )  RATIONAL_B_SPLINE_CURVE ( ( 1.000000000000000000, 0.9999177325257868620, 0.9999177325257868620, 1.000000000000000000 ) ) 
 REPRESENTATION_ITEM ( '' )  );
#133627=ORIENTED_EDGE ( 'NONE', *, *, #20937, .T. ) ;
#133628=VECTOR ( 'NONE', #88883, 1000.000000000000000 ) ;
#133629=FACE_OUTER_BOUND ( 'NONE', #116038, .T. ) ;
#133632=LINE ( 'NONE', #123494, #91757 ) ;
#133633=CARTESIAN_POINT ( 'NONE',  ( 0.000000000000000000, 0.000000000000000000, 5.000000000000000000 ) ) ;
#133634=ADVANCED_FACE ( 'NONE', ( #8346 ), #129440, .F. ) ;
#133638=ORIENTED_EDGE ( 'NONE', *, *, #80303, .F. ) ;
#133639=CARTESIAN_POINT ( 'NONE',  ( 17.99999999999986855, 7.007997736742456851, -8.085015511992068582 ) ) ;
#133640=ORIENTED_EDGE ( 'NONE', *, *, #96489, .T. ) ;
#133641=FACE_OUTER_BOUND ( 'NONE', #22611, .T. ) ;
#133642=CARTESIAN_POINT ( 'NONE',  ( 21.18398860626899349, 28.73617430169802134, 5.000000000000000000 ) ) ;
#133643=VECTOR ( 'NONE', #65136, 1000.000000000000227 ) ;
#133644=DIRECTION ( 'NONE',  ( 1.000000000000000000, 0.000000000000000000, 0.000000000000000000 ) ) ;
#133645=CARTESIAN_POINT ( 'NONE',  ( 32.99999999999977973, -0.4125381241607516403, 4.000000000000000000 ) ) ;
#133646=EDGE_CURVE ( 'NONE', #138878, #93773, #19265, .T. ) ;
#133647=FACE_BOUND ( 'NONE', #5217, .T. ) ;
#133648=DIRECTION ( 'NONE',  ( -0.6830127018922180770, -0.6830127018922204085, -0.2588190451025213501 ) ) ;
#133649=CARTESIAN_POINT ( 'NONE',  ( -66.29974487139159578, -27.71228299555252406, 4.000000000000000000 ) ) ;
#133650=EDGE_CURVE ( 'NONE', #11420, #12388, #86679, .T. ) ;
#133651=CARTESIAN_POINT ( 'NONE',  ( 11.99999999999992006, -4.068876922607777225, 4.000000000000000000 ) ) ;
#133652=FACE_OUTER_BOUND ( 'NONE', #59360, .T. ) ;
#133653=ORIENTED_EDGE ( 'NONE', *, *, #109605, .F. ) ;
#133654=DIRECTION ( 'NONE',  ( -0.6830127018922180770, -0.6830127018922204085, -0.2588190451025213501 ) ) ;
#133655=ORIENTED_EDGE ( 'NONE', *, *, #71559, .T. ) ;
#133656=ORIENTED_EDGE ( 'NONE', *, *, #115636, .F. ) ;
#133659=VECTOR ( 'NONE', #32005, 1000.000000000000000 ) ;
#133660=ADVANCED_FACE ( 'NONE', ( #140330 ), #109118, .F. ) ;
#133661=DIRECTION ( 'NONE',  ( 0.7071067811865486830, -0.7071067811865464625, -0.000000000000000000 ) ) ;
#133662=ORIENTED_EDGE ( 'NONE', *, *, #88842, .F. ) ;
#133663=CARTESIAN_POINT ( 'NONE',  ( -39.18398860626899705, 28.73617430169814568, 5.000000000000000000 ) ) ;
#133664=ADVANCED_FACE ( 'NONE', ( #66357 ), #20675, .F. ) ;
#133665=FACE_OUTER_BOUND ( 'NONE', #22360, .T. ) ;
#133667=LINE ( 'NONE', #134387, #61756 ) ;
#133669=DIRECTION ( 'NONE',  ( -0.7071067811865486830, -0.7071067811865464625, 0.000000000000000000 ) ) ;
#133670=LINE ( 'NONE', #78575, #60939 ) ;
#133671=FACE_OUTER_BOUND ( 'NONE', #40930, .T. ) ;
#133672=ORIENTED_EDGE ( 'NONE', *, *, #72838, .F. ) ;
#133673=EDGE_CURVE ( 'NONE', #26241, #3326, #77252, .T. ) ;
#133674=EDGE_CURVE ( 'NONE', #18494, #11065, #51911, .T. ) ;
#133675=ORIENTED_EDGE ( 'NONE', *, *, #55838, .T. ) ;
#133676=LINE ( 'NONE', #44562, #118414 ) ;
#133677=ORIENTED_EDGE ( 'NONE', *, *, #67931, .T. ) ;
#133678=ORIENTED_EDGE ( 'NONE', *, *, #43942, .T. ) ;
#133679=AXIS2_PLACEMENT_3D ( 'NONE', #75873, #99022, #43252 ) ;
#133680=ORIENTED_EDGE ( 'NONE', *, *, #111958, .T. ) ;
#133682=ORIENTED_EDGE ( 'NONE', *, *, #45362, .T. ) ;
#133683=DIRECTION ( 'NONE',  ( -0.6830127018922181881, 0.6830127018922202975, -0.2588190451025214056 ) ) ;
#133685=VECTOR ( 'NONE', #132960, 1000.000000000000227 ) ;
#133690=EDGE_LOOP ( 'NONE', ( #20770, #111243, #31734, #104483 ) ) ;
#133691=CARTESIAN_POINT ( 'NONE',  ( 6.005480084712508493, 28.92564299267933947, 4.000000000000000000 ) ) ;
#133692=EDGE_CURVE ( 'NONE', #15110, #84993, #143180, .T. ) ;
#133693=DIRECTION ( 'NONE',  ( -0.7071067811865486830, -0.7071067811865464625, -0.000000000000000000 ) ) ;
#133694=AXIS2_PLACEMENT_3D ( 'NONE', #31277, #121637, #79646 ) ;
#133695=CARTESIAN_POINT ( 'NONE',  ( 23.99451991528749062, 28.92564299267954908, 4.000000000000000000 ) ) ;
#133696=CARTESIAN_POINT ( 'NONE',  ( -69.29974487139159578, -27.71228299555254537, 4.000000000000000000 ) ) ;
#133697=ORIENTED_EDGE ( 'NONE', *, *, #101538, .F. ) ;
#133698=EDGE_LOOP ( 'NONE', ( #63555, #26674, #31104, #36473 ) ) ;
#133700=CARTESIAN_POINT ( 'NONE',  ( -11.99999999999991651, -8.731860332648849976, -2.120594902707566565 ) ) ;
#133702=EDGE_CURVE ( 'NONE', #46893, #42124, #37087, .T. ) ;
#133703=LINE ( 'NONE', #91616, #5426 ) ;
#133704=ORIENTED_EDGE ( 'NONE', *, *, #115987, .F. ) ;
#133705=DIRECTION ( 'NONE',  ( 0.7071067811865486830, -0.7071067811865464625, -0.000000000000000000 ) ) ;
#133706=PLANE ( 'NONE',  #29389 ) ;
#133707=ORIENTED_EDGE ( 'NONE', *, *, #7742, .T. ) ;
#133710=CARTESIAN_POINT ( 'NONE',  ( 60.18398860626900415, 28.73617430169829490, 5.000000000000000000 ) ) ;
#133711=DIRECTION ( 'NONE',  ( -0.6830127018922181881, 0.6830127018922202975, -0.2588190451025214056 ) ) ;
#133712=EDGE_CURVE ( 'NONE', #47325, #22051, #91490, .T. ) ;
#133715=LINE ( 'NONE', #3174, #77213 ) ;
#133716=ADVANCED_FACE ( 'NONE', ( #70491 ), #338, .T. ) ;
#133717=DIRECTION ( 'NONE',  ( -0.000000000000000000, 0.3543493200069153248, 0.9351131265310292928 ) ) ;
#133718=ORIENTED_EDGE ( 'NONE', *, *, #91294, .F. ) ;
#133721=VECTOR ( 'NONE', #90166, 1000.000000000000000 ) ;
#133723=LINE ( 'NONE', #67789, #106123 ) ;
#133724=CARTESIAN_POINT ( 'NONE',  ( 9.813491353976328213, -15.74070752338412049, 8.904080028138917413 ) ) ;
#133725=ADVANCED_FACE ( 'NONE', ( #103073 ), #59588, .F. ) ;
#133726=VERTEX_POINT ( 'NONE', #48692 ) ;
#133727=DIRECTION ( 'NONE',  ( -0.3543493200069162685, -0.000000000000000000, -0.9351131265310288487 ) ) ;
#133728=CARTESIAN_POINT ( 'NONE',  ( 23.99999999999983302, -6.033600742197676503, 5.000000000000000000 ) ) ;
#133729=EDGE_CURVE ( 'NONE', #38905, #99727, #49437, .T. ) ;
#133731=VERTEX_POINT ( 'NONE', #135704 ) ;
#133733=LINE ( 'NONE', #136387, #127550 ) ;
#133734=DIRECTION ( 'NONE',  ( -0.7071067811865487940, 0.7071067811865463515, -0.000000000000000000 ) ) ;
#133735=ADVANCED_FACE ( 'NONE', ( #47319 ), #77941, .F. ) ;
#133736=CARTESIAN_POINT ( 'NONE',  ( 9.707013264292969623, -21.74070752338406365, 4.999753212805217117 ) ) ;
#133738=LINE ( 'NONE', #45328, #69661 ) ;
#133739=DIRECTION ( 'NONE',  ( 0.7071067811865487940, 0.7071067811865463515, 0.000000000000000000 ) ) ;
#133741=LINE ( 'NONE', #109109, #139030 ) ;
#133742=ORIENTED_EDGE ( 'NONE', *, *, #4100, .F. ) ;
#133746=CARTESIAN_POINT ( 'NONE',  ( 0.005480084712502889671, 28.92564299267938210, 4.000000000000000000 ) ) ;
#133748=DIRECTION ( 'NONE',  ( 0.7071067811865487940, -0.7071067811865463515, 0.000000000000000000 ) ) ;
#133749=DIRECTION ( 'NONE',  ( 1.000000000000000000, -0.000000000000000000, 0.000000000000000000 ) ) ;
#133750=VERTEX_POINT ( 'NONE', #81341 ) ;
#133751=VERTEX_POINT ( 'NONE', #93626 ) ;
#133752=LINE ( 'NONE', #89523, #136675 ) ;
#133754=DIRECTION ( 'NONE',  ( 0.7071067811865487940, 0.7071067811865463515, 0.000000000000000000 ) ) ;
#133756=EDGE_CURVE ( 'NONE', #69257, #14507, #69030, .T. ) ;
#133758=CARTESIAN_POINT ( 'NONE',  ( -7.823340898400223509, 5.259292476615665457, 15.86257073897099801 ) ) ;
#133759=EDGE_CURVE ( 'NONE', #88152, #130798, #15306, .T. ) ;
#133760=DIRECTION ( 'NONE',  ( -0.7071067811865486830, -0.7071067811865464625, 0.000000000000000000 ) ) ;
#133761=ORIENTED_EDGE ( 'NONE', *, *, #123265, .T. ) ;
#133762=VECTOR ( 'NONE', #16297, 1000.000000000000227 ) ;
#133764=DIRECTION ( 'NONE',  ( -0.7071067811865486830, 0.7071067811865464625, 0.000000000000000000 ) ) ;
#133765=LINE ( 'NONE', #113415, #36938 ) ;
#133766=DIRECTION ( 'NONE',  ( -0.6830127018922181881, 0.6830127018922202975, -0.2588190451025214056 ) ) ;
#133767=VERTEX_POINT ( 'NONE', #99663 ) ;
#133768=EDGE_CURVE ( 'NONE', #77873, #32412, #36388, .T. ) ;
#133769=DIRECTION ( 'NONE',  ( 0.7071067811865486830, -0.7071067811865464625, -0.000000000000000000 ) ) ;
#133770=CARTESIAN_POINT ( 'NONE',  ( -30.48921356237309510, -27.52281430457076894, 5.000000000000000000 ) ) ;
#133772=VERTEX_POINT ( 'NONE', #3706 ) ;
#133773=EDGE_LOOP ( 'NONE', ( #108045, #4832, #14638, #90666 ) ) ;
#133776=FACE_OUTER_BOUND ( 'NONE', #17032, .T. ) ;
#133777=DIRECTION ( 'NONE',  ( -0.7071067811865486830, -0.7071067811865464625, 0.000000000000000000 ) ) ;
#133779=CARTESIAN_POINT ( 'NONE',  ( 60.18398860626900415, 28.73617430169829490, 5.000000000000000000 ) ) ;
#133781=FACE_OUTER_BOUND ( 'NONE', #37767, .T. ) ;
#133782=ORIENTED_EDGE ( 'NONE', *, *, #17798, .F. ) ;
#133785=PLANE ( 'NONE',  #68521 ) ;
#133786=CARTESIAN_POINT ( 'NONE',  ( -23.99999999999982947, -0.1606350220013114671, 4.664761815935120737 ) ) ;
#133787=AXIS2_PLACEMENT_3D ( 'NONE', #128316, #28990, #59499 ) ;
#133788=CARTESIAN_POINT ( 'NONE',  ( 17.51078643762690845, -27.52281430457043143, 5.000000000000000000 ) ) ;
#133790=VERTEX_POINT ( 'NONE', #133053 ) ;
#133791=EDGE_LOOP ( 'NONE', ( #95220, #49716, #24207, #41043 ) ) ;
#133793=VERTEX_POINT ( 'NONE', #37834 ) ;
#133794=CARTESIAN_POINT ( 'NONE',  ( 20.51078643762690490, -27.52281430457041012, 5.000000000000000000 ) ) ;
#133795=LINE ( 'NONE', #68559, #129052 ) ;
#133796=DIRECTION ( 'NONE',  ( 0.7071067811865486830, -0.7071067811865464625, -0.000000000000000000 ) ) ;
#133797=ADVANCED_FACE ( 'NONE', ( #33737 ), #113210, .F. ) ;
#133798=CARTESIAN_POINT ( 'NONE',  ( 30.48921356237309510, -27.52281430457076894, 5.000000000000000000 ) ) ;
#133800=ORIENTED_EDGE ( 'NONE', *, *, #123166, .F. ) ;
#133801=ORIENTED_EDGE ( 'NONE', *, *, #35308, .F. ) ;
#133802=CARTESIAN_POINT ( 'NONE',  ( -3.706792507240715295, 20.25929247661552068, 20.83292124670815681 ) ) ;
#133803=ORIENTED_EDGE ( 'NONE', *, *, #104734, .T. ) ;
#133804=CARTESIAN_POINT ( 'NONE',  ( -29.29289321881324426, 5.259292476615659240, 5.000000000000000000 ) ) ;
#133805=DIRECTION ( 'NONE',  ( -0.7071067811865487940, 0.7071067811865463515, 0.000000000000000000 ) ) ;
#133806=DIRECTION ( 'NONE',  ( 0.7071067811865487940, 0.7071067811865463515, -0.000000000000000000 ) ) ;
#133807=VERTEX_POINT ( 'NONE', #113939 ) ;
#133808=EDGE_CURVE ( 'NONE', #124820, #41591, #92896, .T. ) ;
#133809=EDGE_CURVE ( 'NONE', #135883, #130610, #60302, .T. ) ;
#133810=FACE_BOUND ( 'NONE', #117737, .T. ) ;
#133812=FACE_OUTER_BOUND ( 'NONE', #19650, .T. ) ;
#133813=LINE ( 'NONE', #34499, #80701 ) ;
#133814=VECTOR ( 'NONE', #131168, 999.9999999999998863 ) ;
#133815=CARTESIAN_POINT ( 'NONE',  ( 18.18398860626898994, 28.73617430169800002, 5.000000000000000000 ) ) ;
#133816=EDGE_CURVE ( 'NONE', #53919, #41067, #126251, .T. ) ;
#133818=CARTESIAN_POINT ( 'NONE',  ( 23.67183060077630330, -21.74070752338406365, 4.000000000000000000 ) ) ;
#133820=ORIENTED_EDGE ( 'NONE', *, *, #141389, .F. ) ;
#133821=VERTEX_POINT ( 'NONE', #139295 ) ;
#133823=ORIENTED_EDGE ( 'NONE', *, *, #56373, .F. ) ;
#133826=ORIENTED_EDGE ( 'NONE', *, *, #117336, .F. ) ;
#133827=CARTESIAN_POINT ( 'NONE',  ( -26.84387692260740366, -22.22500000000000142, 4.000000000000000000 ) ) ;
#133830=ADVANCED_FACE ( 'NONE', ( #141402 ), #129809, .F. ) ;
#133831=CARTESIAN_POINT ( 'NONE',  ( 32.99999999999976552, 11.58746187583913390, 4.000000000000000000 ) ) ;
#133832=ORIENTED_EDGE ( 'NONE', *, *, #85932, .F. ) ;
#133833=CARTESIAN_POINT ( 'NONE',  ( 34.47516574401890921, -17.97193265888400049, 4.998110765256835286 ) ) ;
#133836=CARTESIAN_POINT ( 'NONE',  ( -21.18398860626899349, 28.73617430169802134, 5.000000000000000000 ) ) ;
#133839=DIRECTION ( 'NONE',  ( -0.000000000000000000, -0.3543493200069152693, 0.9351131265310292928 ) ) ;
#133840=VERTEX_POINT ( 'NONE', #18155 ) ;
#133841=DIRECTION ( 'NONE',  ( 0.7071067811865486830, -0.7071067811865464625, -0.000000000000000000 ) ) ;
#133842=CARTESIAN_POINT ( 'NONE',  ( 27.18398860626900060, 28.73617430169806042, 5.000000000000000000 ) ) ;
#133843=ORIENTED_EDGE ( 'NONE', *, *, #76096, .T. ) ;
#133844=ORIENTED_EDGE ( 'NONE', *, *, #58646, .F. ) ;
#133845=ORIENTED_EDGE ( 'NONE', *, *, #87128, .T. ) ;
#133847=EDGE_CURVE ( 'NONE', #13520, #65516, #106595, .T. ) ;
#133848=ORIENTED_EDGE ( 'NONE', *, *, #55601, .T. ) ;
#133849=DIRECTION ( 'NONE',  ( -0.000000000000000000, 0.3543493200069153248, 0.9351131265310292928 ) ) ;
#133851=AXIS2_PLACEMENT_3D ( 'NONE', #135123, #122045, #90145 ) ;
#133853=DIRECTION ( 'NONE',  ( 0.7071067811865486830, -0.7071067811865464625, -0.000000000000000000 ) ) ;
#133854=ORIENTED_EDGE ( 'NONE', *, *, #32919, .F. ) ;
#133855=EDGE_CURVE ( 'NONE', #111950, #98883, #51560, .T. ) ;
#133856=ORIENTED_EDGE ( 'NONE', *, *, #74157, .T. ) ;
#133857=CARTESIAN_POINT ( 'NONE',  ( 32.99999999999977973, 14.96639925780211122, 5.000000000000000000 ) ) ;
#133858=CARTESIAN_POINT ( 'NONE',  ( 28.49999999999981171, 8.319652575858409449, -8.582050562765761725 ) ) ;
#133860=FACE_OUTER_BOUND ( 'NONE', #12585, .T. ) ;
#133862=DIRECTION ( 'NONE',  ( -0.7071067811865486830, 0.7071067811865464625, 0.000000000000000000 ) ) ;
#133863=EDGE_CURVE ( 'NONE', #132022, #116559, #39989, .T. ) ;
#133864=ORIENTED_EDGE ( 'NONE', *, *, #1120, .F. ) ;
#133866=PLANE ( 'NONE',  #47545 ) ;
#133867=ORIENTED_EDGE ( 'NONE', *, *, #64623, .T. ) ;
#133868=EDGE_CURVE ( 'NONE', #48369, #108055, #29078, .T. ) ;
#133870=VERTEX_POINT ( 'NONE', #16767 ) ;
#133871=DIRECTION ( 'NONE',  ( -0.3543493200069162685, -0.000000000000000000, -0.9351131265310288487 ) ) ;
#133873=ADVANCED_FACE ( 'NONE', ( #138558 ), #28376, .F. ) ;
#133875=AXIS2_PLACEMENT_3D ( 'NONE', #51816, #104745, #59835 ) ;
#133876=PLANE ( 'NONE',  #53222 ) ;
#133877=DIRECTION ( 'NONE',  ( -0.7071067811865486830, -0.7071067811865464625, 0.000000000000000000 ) ) ;
#133878=VERTEX_POINT ( 'NONE', #116791 ) ;
#133879=VECTOR ( 'NONE', #83201, 1000.000000000000000 ) ;
#133884=CARTESIAN_POINT ( 'NONE',  ( -29.99999999999979039, 2.342191155542419523, -5.001666872980017331 ) ) ;
#133885=EDGE_CURVE ( 'NONE', #18576, #96758, #17474, .T. ) ;
#133886=LINE ( 'NONE', #34578, #37401 ) ;
#133887=ORIENTED_EDGE ( 'NONE', *, *, #79226, .T. ) ;
#133888=ORIENTED_EDGE ( 'NONE', *, *, #6500, .F. ) ;
#133889=VERTEX_POINT ( 'NONE', #74015 ) ;
#133891=FACE_BOUND ( 'NONE', #48482, .T. ) ;
#133892=AXIS2_PLACEMENT_3D ( 'NONE', #78457, #22597, #68326 ) ;
#133893=CARTESIAN_POINT ( 'NONE',  ( -66.18398860626901126, 28.73617430169833753, 5.000000000000000000 ) ) ;
#133894=ADVANCED_FACE ( 'NONE', ( #6552 ), #18902, .F. ) ;
#133895=LINE ( 'NONE', #34586, #78413 ) ;
#133897=LINE ( 'NONE', #72262, #120099 ) ;
#133898=CARTESIAN_POINT ( 'NONE',  ( -27.18398860626900060, 28.73617430169806042, 5.000000000000000000 ) ) ;
#133899=LINE ( 'NONE', #12812, #16253 ) ;
#133900=CARTESIAN_POINT ( 'NONE',  ( -39.29974487139159578, -27.71228299555233576, 4.000000000000000000 ) ) ;
#133901=ORIENTED_EDGE ( 'NONE', *, *, #7118, .F. ) ;
#133903=VERTEX_POINT ( 'NONE', #42829 ) ;
#133906=VECTOR ( 'NONE', #2456, 1000.000000000000227 ) ;
#133907=AXIS2_PLACEMENT_3D ( 'NONE', #107265, #76084, #7942 ) ;
#133909=CARTESIAN_POINT ( 'NONE',  ( 0.000000000000000000, 0.000000000000000000, 5.000000000000000000 ) ) ;
#133910=VERTEX_POINT ( 'NONE', #10166 ) ;
#133911=CARTESIAN_POINT ( 'NONE',  ( 6.938893903907228378E-15, -3.412538124160723108, 4.000000000000000000 ) ) ;
#133912=DIRECTION ( 'NONE',  ( 0.7071067811865487940, 0.7071067811865463515, 0.000000000000000000 ) ) ;
#133913=VERTEX_POINT ( 'NONE', #43520 ) ;
#133916=DIRECTION ( 'NONE',  ( 0.000000000000000000, -1.000000000000000000, 0.000000000000000000 ) ) ;
#133917=EDGE_LOOP ( 'NONE', ( #43297, #18447, #108447, #82281 ) ) ;
#133918=DIRECTION ( 'NONE',  ( 0.7071067811865486830, -0.7071067811865464625, -0.000000000000000000 ) ) ;
#133919=ADVANCED_FACE ( 'NONE', ( #707 ), #132714, .T. ) ;
#133923=ORIENTED_EDGE ( 'NONE', *, *, #81776, .F. ) ;
#133924=CARTESIAN_POINT ( 'NONE',  ( 12.18398860626900060, 28.73617430169795739, 5.000000000000000000 ) ) ;
#133925=LINE ( 'NONE', #74205, #88968 ) ;
#133926=DIRECTION ( 'NONE',  ( 0.7071067811865487940, 0.7071067811865463515, 0.000000000000000000 ) ) ;
#133929=VECTOR ( 'NONE', #18078, 1000.000000000000000 ) ;
#133930=DIRECTION ( 'NONE',  ( 0.7071067811865486830, -0.7071067811865464625, -0.000000000000000000 ) ) ;
#133932=ORIENTED_EDGE ( 'NONE', *, *, #55829, .T. ) ;
#133933=AXIS2_PLACEMENT_3D ( 'NONE', #94484, #61218, #38699 ) ;
#133934=ORIENTED_EDGE ( 'NONE', *, *, #42137, .F. ) ;
#133935=CARTESIAN_POINT ( 'NONE',  ( 2.010880286539464379, -22.02621442084248216, 4.990779571109223767 ) ) ;
#133936=ORIENTED_EDGE ( 'NONE', *, *, #13743, .F. ) ;
#133938=DIRECTION ( 'NONE',  ( 0.6830127018922181881, 0.6830127018922202975, -0.2588190451025214056 ) ) ;
#133939=DIRECTION ( 'NONE',  ( -0.7071067811865487940, 0.7071067811865463515, -0.000000000000000000 ) ) ;
#133940=CARTESIAN_POINT ( 'NONE',  ( -34.92500000000001137, -7.199905483972716347, 4.759050581649336920 ) ) ;
#133942=ORIENTED_EDGE ( 'NONE', *, *, #92692, .F. ) ;
#133943=CARTESIAN_POINT ( 'NONE',  ( 28.49999999999980460, -20.53675388469227769, 2.352720554255958607 ) ) ;
#133944=DIRECTION ( 'NONE',  ( 0.3543493200069163240, -0.000000000000000000, 0.9351131265310288487 ) ) ;
#133945=LINE ( 'NONE', #113603, #44282 ) ;
#133946=DIRECTION ( 'NONE',  ( 0.7071067811865487940, 0.7071067811865463515, 0.000000000000000000 ) ) ;
#133947=PLANE ( 'NONE',  #68397 ) ;
#133950=LINE ( 'NONE', #123088, #22204 ) ;
#133951=CARTESIAN_POINT ( 'NONE',  ( -24.79289321881327979, -8.240707523384198652, 5.000000000000000000 ) ) ;
#133952=DIRECTION ( 'NONE',  ( -0.6830127018922180770, -0.6830127018922204085, -0.2588190451025213501 ) ) ;
#133953=CARTESIAN_POINT ( 'NONE',  ( 22.49999999999984723, 15.43112307739202826, 4.000000000000000000 ) ) ;
#133954=EDGE_LOOP ( 'NONE', ( #133442, #121748, #26297, #120111 ) ) ;
#133955=ORIENTED_EDGE ( 'NONE', *, *, #128477, .F. ) ;
#133956=ORIENTED_EDGE ( 'NONE', *, *, #105693, .T. ) ;
#133958=EDGE_LOOP ( 'NONE', ( #15993, #7689, #85190, #111152 ) ) ;
#133959=CARTESIAN_POINT ( 'NONE',  ( 31.49999999999978684, 3.052185695429138423, 5.000000000000000000 ) ) ;
#133961=CARTESIAN_POINT ( 'NONE',  ( 50.99451991528749062, 28.92564299267973738, 4.000000000000000000 ) ) ;
#133962=CARTESIAN_POINT ( 'NONE',  ( -63.48921356237309510, -27.52281430457099631, 5.000000000000000000 ) ) ;
#133963=ORIENTED_EDGE ( 'NONE', *, *, #36337, .F. ) ;
#133964=FACE_OUTER_BOUND ( 'NONE', #94783, .T. ) ;
#133965=CARTESIAN_POINT ( 'NONE',  ( 1.499999999999994449, 3.073033219394626592, -6.593910359670966947 ) ) ;
#133966=LINE ( 'NONE', #24487, #125166 ) ;
#133968=EDGE_LOOP ( 'NONE', ( #33902, #34257, #54372, #89135 ) ) ;
#133969=DIRECTION ( 'NONE',  ( 0.6830127018922180770, -0.6830127018922204085, -0.2588190451025213501 ) ) ;
#133970=ADVANCED_FACE ( 'NONE', ( #45697 ), #143544, .F. ) ;
#133971=EDGE_CURVE ( 'NONE', #74639, #25093, #56594, .T. ) ;
#133973=VECTOR ( 'NONE', #109927, 1000.000000000000227 ) ;
#133974=AXIS2_PLACEMENT_3D ( 'NONE', #103366, #59217, #79556 ) ;
#133975=VECTOR ( 'NONE', #95645, 1000.000000000000227 ) ;
#133976=ORIENTED_EDGE ( 'NONE', *, *, #106933, .T. ) ;
#133978=AXIS2_PLACEMENT_3D ( 'NONE', #131680, #122195, #41810 ) ;
#133979=DIRECTION ( 'NONE',  ( -0.7071067811865486830, -0.7071067811865464625, -0.000000000000000000 ) ) ;
#133980=EDGE_CURVE ( 'NONE', #16744, #49722, #109491, .T. ) ;
#133981=ADVANCED_FACE ( 'NONE', ( #20315 ), #23164, .F. ) ;
#133984=CARTESIAN_POINT ( 'NONE',  ( -47.99451991528749062, 28.92564299267971251, 4.000000000000000000 ) ) ;
#133986=AXIS2_PLACEMENT_3D ( 'NONE', #96187, #128835, #16487 ) ;
#133987=DIRECTION ( 'NONE',  ( 0.7071067811865487940, -0.7071067811865463515, 0.000000000000000000 ) ) ;
#133988=DIRECTION ( 'NONE',  ( -0.7071067811865487940, 0.7071067811865463515, 0.000000000000000000 ) ) ;
#133989=EDGE_CURVE ( 'NONE', #92202, #70018, #78301, .T. ) ;
#133990=ADVANCED_FACE ( 'NONE', ( #108738 ), #9419, .F. ) ;
#133991=PLANE ( 'NONE',  #121470 ) ;
#133992=VERTEX_POINT ( 'NONE', #131244 ) ;
#133993=( BOUNDED_CURVE ( )  B_SPLINE_CURVE ( 3, ( #53225, #65593, #43801, #88017 ),
 .UNSPECIFIED., .F., .F. ) 
 B_SPLINE_CURVE_WITH_KNOTS ( ( 4, 4 ),
 ( 5.005968288816738720, 5.074607125596333645 ),
 .UNSPECIFIED. ) 
 CURVE ( )  GEOMETRIC_REPRESENTATION_ITEM ( )  RATIONAL_B_SPLINE_CURVE ( ( 1.000000000000000000, 0.9996074310407766506, 0.9996074310407766506, 1.000000000000000000 ) ) 
 REPRESENTATION_ITEM ( '' )  );
#133995=CARTESIAN_POINT ( 'NONE',  ( 3.469446951953614189E-15, 8.587461875839158765, 4.000000000000000000 ) ) ;
#133996=EDGE_CURVE ( 'NONE', #63182, #25281, #65269, .T. ) ;
#133997=ORIENTED_EDGE ( 'NONE', *, *, #25090, .T. ) ;
#133998=ORIENTED_EDGE ( 'NONE', *, *, #52468, .T. ) ;
#133999=VECTOR ( 'NONE', #118912, 1000.000000000000000 ) ;
#134001=EDGE_CURVE ( 'NONE', #72640, #80026, #122489, .T. ) ;
#134003=DIRECTION ( 'NONE',  ( -0.000000000000000000, 0.3543493200069153248, 0.9351131265310292928 ) ) ;
#134004=VERTEX_POINT ( 'NONE', #12309 ) ;
#134005=CARTESIAN_POINT ( 'NONE',  ( -15.18398860626900237, 28.73617430169797871, 5.000000000000000000 ) ) ;
#134006=DIRECTION ( 'NONE',  ( -0.7071067811865487940, 0.7071067811865463515, 0.000000000000000000 ) ) ;
#134007=DIRECTION ( 'NONE',  ( 1.000000000000000000, 0.000000000000000000, 0.000000000000000000 ) ) ;
#134009=AXIS2_PLACEMENT_3D ( 'NONE', #9416, #43518, #108025 ) ;
#134011=LINE ( 'NONE', #57192, #37551 ) ;
#134012=ORIENTED_EDGE ( 'NONE', *, *, #96784, .T. ) ;
#134013=VECTOR ( 'NONE', #70978, 1000.000000000000000 ) ;
#134014=EDGE_CURVE ( 'NONE', #59677, #70620, #133404, .T. ) ;
#134016=VECTOR ( 'NONE', #137478, 1000.000000000000227 ) ;
#134019=ORIENTED_EDGE ( 'NONE', *, *, #113327, .T. ) ;
#134020=CARTESIAN_POINT ( 'NONE',  ( 5.671830600776431197, -12.74070752338415424, 4.000000000000000000 ) ) ;
#134021=VERTEX_POINT ( 'NONE', #32660 ) ;
#134022=LINE ( 'NONE', #34711, #29652 ) ;
#134023=EDGE_LOOP ( 'NONE', ( #129940, #114905, #38558, #108831 ) ) ;
#134024=ORIENTED_EDGE ( 'NONE', *, *, #120773, .T. ) ;
#134025=AXIS2_PLACEMENT_3D ( 'NONE', #112351, #68865, #70316 ) ;
#134026=EDGE_CURVE ( 'NONE', #36664, #58070, #54653, .T. ) ;
#134027=ORIENTED_EDGE ( 'NONE', *, *, #39591, .F. ) ;
#134029=PLANE ( 'NONE',  #129963 ) ;
#134030=DIRECTION ( 'NONE',  ( 0.7071067811865486830, -0.7071067811865464625, -0.000000000000000000 ) ) ;
#134031=CARTESIAN_POINT ( 'NONE',  ( 0.7928932188134545367, 3.759292476615681888, 5.000000000000000000 ) ) ;
#134032=DIRECTION ( 'NONE',  ( -0.6830127018922180770, -0.6830127018922204085, -0.2588190451025213501 ) ) ;
#134034=FACE_OUTER_BOUND ( 'NONE', #123044, .T. ) ;
#134035=CARTESIAN_POINT ( 'NONE',  ( 8.994519915287490619, 28.92564299267944250, 4.000000000000000000 ) ) ;
#134036=LINE ( 'NONE', #33331, #136181 ) ;
#134037=EDGE_CURVE ( 'NONE', #129523, #99824, #121774, .T. ) ;
#134038=VECTOR ( 'NONE', #93056, 1000.000000000000227 ) ;
#134039=FACE_OUTER_BOUND ( 'NONE', #54056, .T. ) ;
#134041=EDGE_CURVE ( 'NONE', #137069, #50477, #11569, .T. ) ;
#134043=CARTESIAN_POINT ( 'NONE',  ( 1.903119261757429959, -22.22500000000000142, -8.955551095671996364 ) ) ;
#134044=DIRECTION ( 'NONE',  ( -0.7071067811865487940, 0.7071067811865463515, 0.000000000000000000 ) ) ;
#134045=CARTESIAN_POINT ( 'NONE',  ( 14.99451991528749595, 28.92564299267948513, 4.000000000000000000 ) ) ;
#134046=ORIENTED_EDGE ( 'NONE', *, *, #143215, .F. ) ;
#134047=ADVANCED_FACE ( 'NONE', ( #34093 ), #23924, .T. ) ;
#134049=FACE_OUTER_BOUND ( 'NONE', #122080, .T. ) ;
#134050=ORIENTED_EDGE ( 'NONE', *, *, #90629, .F. ) ;
#134051=EDGE_CURVE ( 'NONE', #103176, #50701, #26759, .T. ) ;
#134052=EDGE_CURVE ( 'NONE', #67739, #88536, #13715, .T. ) ;
#134053=ORIENTED_EDGE ( 'NONE', *, *, #128054, .F. ) ;
#134054=CARTESIAN_POINT ( 'NONE',  ( -18.00548008471250583, 28.92564299267925776, 4.000000000000000000 ) ) ;
#134055=CARTESIAN_POINT ( 'NONE',  ( 26.20710678118636494, 15.75929247661556687, 5.000000000000000000 ) ) ;
#134056=CARTESIAN_POINT ( 'NONE',  ( 0.005480084712502889671, 28.92564299267938210, 4.000000000000000000 ) ) ;
#134057=DIRECTION ( 'NONE',  ( -0.7071067811865487940, 0.7071067811865463515, 0.000000000000000000 ) ) ;
#134058=VERTEX_POINT ( 'NONE', #15148 ) ;
#134059=DIRECTION ( 'NONE',  ( 0.7071067811865486830, -0.7071067811865464625, -0.000000000000000000 ) ) ;
#134060=ORIENTED_EDGE ( 'NONE', *, *, #45204, .F. ) ;
#134061=CARTESIAN_POINT ( 'NONE',  ( 42.29974487139158157, -27.71228299555235708, 4.000000000000000000 ) ) ;
#134063=EDGE_LOOP ( 'NONE', ( #9181, #111866, #2447, #81806 ) ) ;
#134066=EDGE_CURVE ( 'NONE', #63600, #134564, #81165, .T. ) ;
#134067=PLANE ( 'NONE',  #39598 ) ;
#134068=EDGE_LOOP ( 'NONE', ( #111945, #84120, #17291, #135792 ) ) ;
#134069=EDGE_LOOP ( 'NONE', ( #85250, #84274, #78339, #133718 ) ) ;
#134070=EDGE_LOOP ( 'NONE', ( #72106, #24342, #21505, #21168 ) ) ;
#134071=LINE ( 'NONE', #87699, #54273 ) ;
#134073=DIRECTION ( 'NONE',  ( -0.000000000000000000, 0.000000000000000000, 1.000000000000000000 ) ) ;
#134074=CARTESIAN_POINT ( 'NONE',  ( 29.20710678118634007, -11.24070752338416668, 5.000000000000000000 ) ) ;
#134075=CARTESIAN_POINT ( 'NONE',  ( -11.20710678118646442, 18.75929247661552779, 5.000000000000000000 ) ) ;
#134077=DIRECTION ( 'NONE',  ( 0.7071067811865487940, 0.7071067811865463515, -0.000000000000000000 ) ) ;
#134078=ADVANCED_FACE ( 'NONE', ( #59430 ), #2856, .F. ) ;
#134079=LINE ( 'NONE', #134815, #44558 ) ;
#134080=ORIENTED_EDGE ( 'NONE', *, *, #105988, .T. ) ;
#134081=DIRECTION ( 'NONE',  ( 0.6830127018922180770, -0.6830127018922204085, -0.2588190451025213501 ) ) ;
#134082=VECTOR ( 'NONE', #11850, 1000.000000000000000 ) ;
#134083=VECTOR ( 'NONE', #58087, 1000.000000000000000 ) ;
#134086=ORIENTED_EDGE ( 'NONE', *, *, #93477, .F. ) ;
#134087=AXIS2_PLACEMENT_3D ( 'NONE', #1319, #66615, #43427 ) ;
#134088=PLANE ( 'NONE',  #132018 ) ;
#134089=ORIENTED_EDGE ( 'NONE', *, *, #94554, .F. ) ;
#134090=ADVANCED_FACE ( 'NONE', ( #37663 ), #4222, .T. ) ;
#134091=EDGE_LOOP ( 'NONE', ( #91425, #86336, #4398 ) ) ;
#134092=CARTESIAN_POINT ( 'NONE',  ( -23.99999999999983302, 15.45873954670183359, -0.03131636524288453072 ) ) ;
#134094=ORIENTED_EDGE ( 'NONE', *, *, #127521, .F. ) ;
#134098=PLANE ( 'NONE',  #126222 ) ;
#134099=LINE ( 'NONE', #2096, #127285 ) ;
#134100=EDGE_CURVE ( 'NONE', #22612, #117925, #47848, .T. ) ;
#134101=CARTESIAN_POINT ( 'NONE',  ( -13.17183060077637968, 12.75929247661559351, 4.000000000000000000 ) ) ;
#134104=CARTESIAN_POINT ( 'NONE',  ( -14.99999999999989164, 13.55218569542902607, 5.000000000000000000 ) ) ;
#134105=CARTESIAN_POINT ( 'NONE',  ( -1.033400323430223811, 6.759292476615649470, 12.28218704918521809 ) ) ;
#134106=CARTESIAN_POINT ( 'NONE',  ( 23.24139925780185223, 21.72500000000000853, 5.000000000000000000 ) ) ;
#134109=VECTOR ( 'NONE', #24431, 1000.000000000000227 ) ;
#134110=LINE ( 'NONE', #100052, #64459 ) ;
#134112=CARTESIAN_POINT ( 'NONE',  ( 24.29974487139158867, -27.71228299555223273, 4.000000000000000000 ) ) ;
#134113=CARTESIAN_POINT ( 'NONE',  ( 38.71998032010573354, 0.7592924766157138627, 14.27032725228017895 ) ) ;
#134114=ORIENTED_EDGE ( 'NONE', *, *, #35906, .T. ) ;
#134115=ADVANCED_FACE ( 'NONE', ( #112355 ), #36230, .F. ) ;
#134116=EDGE_LOOP ( 'NONE', ( #119958, #55525, #14166, #90438 ) ) ;
#134118=ADVANCED_FACE ( 'NONE', ( #2110 ), #91334, .T. ) ;
#134119=ORIENTED_EDGE ( 'NONE', *, *, #77906, .T. ) ;
#134120=VERTEX_POINT ( 'NONE', #92013 ) ;
#134122=CARTESIAN_POINT ( 'NONE',  ( -2.999999999999981792, 20.70535890316561023, 1.956823837851923598 ) ) ;
#134123=PLANE ( 'NONE',  #111192 ) ;
#134125=ORIENTED_EDGE ( 'NONE', *, *, #51855, .T. ) ;
#134129=VECTOR ( 'NONE', #133739, 999.9999999999998863 ) ;
#134130=FACE_OUTER_BOUND ( 'NONE', #20890, .T. ) ;
#134131=ORIENTED_EDGE ( 'NONE', *, *, #89533, .T. ) ;
#134133=DIRECTION ( 'NONE',  ( -0.7071067811865486830, -0.7071067811865464625, 0.000000000000000000 ) ) ;
#134134=CARTESIAN_POINT ( 'NONE',  ( -35.99451991528749772, 28.92564299267963079, 4.000000000000000000 ) ) ;
#134135=PLANE ( 'NONE',  #100032 ) ;
#134136=VECTOR ( 'NONE', #75127, 1000.000000000000000 ) ;
#134137=LINE ( 'NONE', #2881, #40663 ) ;
#134138=LINE ( 'NONE', #123275, #67856 ) ;
#134139=DIRECTION ( 'NONE',  ( 0.7071067811865486830, -0.7071067811865464625, -0.000000000000000000 ) ) ;
#134141=DIRECTION ( 'NONE',  ( 0.6830127018922180770, -0.6830127018922204085, -0.2588190451025213501 ) ) ;
#134142=FACE_OUTER_BOUND ( 'NONE', #72044, .T. ) ;
#134143=ORIENTED_EDGE ( 'NONE', *, *, #4876, .T. ) ;
#134144=ORIENTED_EDGE ( 'NONE', *, *, #118390, .T. ) ;
#134146=ORIENTED_EDGE ( 'NONE', *, *, #32757, .T. ) ;
#134149=CARTESIAN_POINT ( 'NONE',  ( -15.70710678118642711, -12.74070752338415069, 5.000000000000000000 ) ) ;
#134150=CARTESIAN_POINT ( 'NONE',  ( -10.49999999999992184, -10.04351517176479014, -1.623559851933848330 ) ) ;
#134153=ORIENTED_EDGE ( 'NONE', *, *, #40698, .F. ) ;
#134154=EDGE_CURVE ( 'NONE', #83338, #28064, #104296, .T. ) ;
#134155=VERTEX_POINT ( 'NONE', #34801 ) ;
#134156=LINE ( 'NONE', #13055, #112578 ) ;
#134158=ORIENTED_EDGE ( 'NONE', *, *, #75739, .T. ) ;
#134159=EDGE_LOOP ( 'NONE', ( #80515, #132950, #71178, #122231, #136358 ) ) ;
#134160=CARTESIAN_POINT ( 'NONE',  ( 42.29974487139158157, -27.71228299555235708, 4.000000000000000000 ) ) ;
#134161=EDGE_CURVE ( 'NONE', #40586, #69387, #57287, .T. ) ;
#134163=ADVANCED_FACE ( 'NONE', ( #135545 ), #80456, .F. ) ;
#134164=EDGE_CURVE ( 'NONE', #69243, #138595, #113772, .T. ) ;
#134166=EDGE_CURVE ( 'NONE', #121813, #116985, #124646, .T. ) ;
#134168=DIRECTION ( 'NONE',  ( 0.7071067811865487940, 0.7071067811865463515, 0.000000000000000000 ) ) ;
#134169=ADVANCED_FACE ( 'NONE', ( #25323 ), #69589, .T. ) ;
#134170=ORIENTED_EDGE ( 'NONE', *, *, #67133, .F. ) ;
#134171=EDGE_LOOP ( 'NONE', ( #95114, #128363, #813, #120065 ) ) ;
#134173=EDGE_CURVE ( 'NONE', #56006, #52354, #28909, .T. ) ;
#134174=EDGE_CURVE ( 'NONE', #65622, #137194, #127503, .T. ) ;
#134175=DIRECTION ( 'NONE',  ( 0.7071067811865487940, -0.7071067811865463515, 0.000000000000000000 ) ) ;
#134177=EDGE_LOOP ( 'NONE', ( #15105, #16909, #131480, #109943, #97890, #88502 ) ) ;
#134178=FACE_OUTER_BOUND ( 'NONE', #47168, .T. ) ;
#134179=ADVANCED_FACE ( 'NONE', ( #7845 ), #62261, .F. ) ;
#134180=AXIS2_PLACEMENT_3D ( 'NONE', #110425, #122019, #133644 ) ;
#134181=DIRECTION ( 'NONE',  ( 0.3543493200069162685, -0.000000000000000000, -0.9351131265310288487 ) ) ;
#134183=AXIS2_PLACEMENT_3D ( 'NONE', #58873, #97, #88607 ) ;
#134184=CARTESIAN_POINT ( 'NONE',  ( 28.49999999999981171, -14.94781430457067550, 5.000000000000000000 ) ) ;
#134185=VECTOR ( 'NONE', #59170, 1000.000000000000227 ) ;
#134186=EDGE_CURVE ( 'NONE', #126057, #50446, #27451, .T. ) ;
#134187=FACE_BOUND ( 'NONE', #685, .T. ) ;
#134188=ORIENTED_EDGE ( 'NONE', *, *, #80572, .T. ) ;
#134191=PLANE ( 'NONE',  #115500 ) ;
#134192=CARTESIAN_POINT ( 'NONE',  ( -32.54016161050240186, 18.75929247661552424, 8.305906642995411815 ) ) ;
#134193=CARTESIAN_POINT ( 'NONE',  ( -34.92500000000001137, 22.22500000000000142, 5.000000000000000000 ) ) ;
#134194=EDGE_LOOP ( 'NONE', ( #102083, #18464, #106481, #88031 ) ) ;
#134195=CARTESIAN_POINT ( 'NONE',  ( 25.49999999999982592, -4.796895815300992183, -3.611700055028623790 ) ) ;
#134196=ORIENTED_EDGE ( 'NONE', *, *, #45840, .F. ) ;
#134197=ORIENTED_EDGE ( 'NONE', *, *, #111637, .F. ) ;
#134198=EDGE_CURVE ( 'NONE', #70580, #33680, #117314, .T. ) ;
#134199=ORIENTED_EDGE ( 'NONE', *, *, #121299, .T. ) ;
#134201=ORIENTED_EDGE ( 'NONE', *, *, #133389, .T. ) ;
#134202=VECTOR ( 'NONE', #141561, 1000.000000000000000 ) ;
#134203=DIRECTION ( 'NONE',  ( -0.7071067811865486830, -0.7071067811865464625, 0.000000000000000000 ) ) ;
#134205=EDGE_LOOP ( 'NONE', ( #13127, #91198, #37349, #55077 ) ) ;
#134206=CARTESIAN_POINT ( 'NONE',  ( -51.18398860626899705, 28.73617430169823095, 5.000000000000000000 ) ) ;
#134207=LINE ( 'NONE', #12402, #99020 ) ;
#134209=CIRCLE ( 'NONE', #60225, 0.5000000000000000000 ) ;
#134211=PLANE ( 'NONE',  #50251 ) ;
#134212=LINE ( 'NONE', #79147, #18109 ) ;
#134215=VERTEX_POINT ( 'NONE', #94846 ) ;
#134218=ORIENTED_EDGE ( 'NONE', *, *, #50078, .T. ) ;
#134219=ORIENTED_EDGE ( 'NONE', *, *, #14392, .F. ) ;
#134220=AXIS2_PLACEMENT_3D ( 'NONE', #82127, #126301, #115380 ) ;
#134221=CARTESIAN_POINT ( 'NONE',  ( -17.99451991528748351, 28.92564299267950645, 4.000000000000000000 ) ) ;
#134222=ORIENTED_EDGE ( 'NONE', *, *, #102941, .F. ) ;
#134224=VERTEX_POINT ( 'NONE', #128233 ) ;
#134226=AXIS2_PLACEMENT_3D ( 'NONE', #66061, #10901, #77646 ) ;
#134227=DIRECTION ( 'NONE',  ( 0.7071067811865487940, 0.7071067811865463515, 0.000000000000000000 ) ) ;
#134228=ORIENTED_EDGE ( 'NONE', *, *, #49619, .F. ) ;
#134229=VECTOR ( 'NONE', #86530, 1000.000000000000000 ) ;
#134230=DIRECTION ( 'NONE',  ( 0.7071067811865487940, 0.7071067811865463515, 0.000000000000000000 ) ) ;
#134231=EDGE_CURVE ( 'NONE', #53824, #24327, #17306, .T. ) ;
#134232=CARTESIAN_POINT ( 'NONE',  ( -8.200031220168323642, 8.259292476615634371, 16.85664084051843048 ) ) ;
#134234=CARTESIAN_POINT ( 'NONE',  ( 25.17183060077629619, -2.240707523384255939, 4.000000000000000000 ) ) ;
#134235=VERTEX_POINT ( 'NONE', #7106 ) ;
#134237=LINE ( 'NONE', #79173, #67558 ) ;
#134238=EDGE_CURVE ( 'NONE', #92174, #126797, #52086, .T. ) ;
#134239=DIRECTION ( 'NONE',  ( -0.000000000000000000, 0.000000000000000000, 1.000000000000000000 ) ) ;
#134242=CARTESIAN_POINT ( 'NONE',  ( 54.18398860626899705, 28.73617430169825226, 5.000000000000000000 ) ) ;
#134243=ORIENTED_EDGE ( 'NONE', *, *, #33880, .F. ) ;
#134244=LINE ( 'NONE', #45125, #20840 ) ;
#134246=FACE_OUTER_BOUND ( 'NONE', #52253, .T. ) ;
#134247=CARTESIAN_POINT ( 'NONE',  ( 34.92499999999998295, 3.759292476615685441, 4.255531930566164078 ) ) ;
#134251=EDGE_CURVE ( 'NONE', #71156, #69437, #96262, .T. ) ;
#134253=LINE ( 'NONE', #44412, #127841 ) ;
#134254=VERTEX_POINT ( 'NONE', #95579 ) ;
#134255=VECTOR ( 'NONE', #55239, 1000.000000000000000 ) ;
#134256=DIRECTION ( 'NONE',  ( -0.000000000000000000, -0.3543493200069152693, 0.9351131265310292928 ) ) ;
#134257=VERTEX_POINT ( 'NONE', #30331 ) ;
#134258=LINE ( 'NONE', #23320, #129465 ) ;
#134259=DIRECTION ( 'NONE',  ( 0.7071067811865487940, 0.7071067811865463515, 0.000000000000000000 ) ) ;
#134260=ORIENTED_EDGE ( 'NONE', *, *, #123066, .F. ) ;
#134261=EDGE_CURVE ( 'NONE', #82848, #10331, #140508, .T. ) ;
#134262=ORIENTED_EDGE ( 'NONE', *, *, #15182, .T. ) ;
#134263=CARTESIAN_POINT ( 'NONE',  ( 42.18398860626899705, 28.73617430169816700, 5.000000000000000000 ) ) ;
#134264=CARTESIAN_POINT ( 'NONE',  ( -9.183988606268997046, 28.73617430169793607, 5.000000000000000000 ) ) ;
#134265=ORIENTED_EDGE ( 'NONE', *, *, #40518, .T. ) ;
#134266=CARTESIAN_POINT ( 'NONE',  ( -22.49999999999984723, 15.43112307739202826, 4.000000000000000000 ) ) ;
#134267=FACE_OUTER_BOUND ( 'NONE', #102208, .T. ) ;
#134268=LINE ( 'NONE', #98755, #67757 ) ;
#134269=EDGE_LOOP ( 'NONE', ( #13661, #85178, #22319, #34764 ) ) ;
#134270=DIRECTION ( 'NONE',  ( 0.7071067811865487940, 0.7071067811865463515, 0.000000000000000000 ) ) ;
#134271=LINE ( 'NONE', #101623, #7332 ) ;
#134272=DIRECTION ( 'NONE',  ( -0.7071067811865487940, 0.7071067811865463515, -0.000000000000000000 ) ) ;
#134273=CARTESIAN_POINT ( 'NONE',  ( -30.48921356237309510, -27.52281430457076894, 5.000000000000000000 ) ) ;
#134275=CARTESIAN_POINT ( 'NONE',  ( -48.29974487139158867, -27.71228299555239971, 4.000000000000000000 ) ) ;
#134276=ORIENTED_EDGE ( 'NONE', *, *, #43091, .F. ) ;
#134278=ORIENTED_EDGE ( 'NONE', *, *, #141542, .T. ) ;
#134279=LINE ( 'NONE', #112517, #83649 ) ;
#134281=EDGE_CURVE ( 'NONE', #11065, #117806, #19451, .T. ) ;
#134282=EDGE_LOOP ( 'NONE', ( #92604, #118499, #86566, #51937 ) ) ;
#134283=VERTEX_POINT ( 'NONE', #41195 ) ;
#134285=VECTOR ( 'NONE', #1630, 1000.000000000000000 ) ;
#134286=DIRECTION ( 'NONE',  ( 0.7071067811865487940, 0.7071067811865463515, 0.000000000000000000 ) ) ;
#134289=VECTOR ( 'NONE', #52227, 1000.000000000000000 ) ;
#134290=VECTOR ( 'NONE', #52897, 1000.000000000000227 ) ;
#134291=ORIENTED_EDGE ( 'NONE', *, *, #89116, .F. ) ;
#134292=( BOUNDED_CURVE ( )  B_SPLINE_CURVE ( 3, ( #62005, #38103, #93883, #6832 ),
 .UNSPECIFIED., .F., .T. ) 
 B_SPLINE_CURVE_WITH_KNOTS ( ( 4, 4 ),
 ( 5.005968288816749379, 5.074607125596352297 ),
 .UNSPECIFIED. ) 
 CURVE ( )  GEOMETRIC_REPRESENTATION_ITEM ( )  RATIONAL_B_SPLINE_CURVE ( ( 1.000000000000000000, 0.9996074310407765395, 0.9996074310407765395, 1.000000000000000000 ) ) 
 REPRESENTATION_ITEM ( '' )  );
#134293=CARTESIAN_POINT ( 'NONE',  ( 24.29974487139158867, -27.71228299555223273, 4.000000000000000000 ) ) ;
#134296=DIRECTION ( 'NONE',  ( 1.000000000000000000, 0.000000000000000000, 0.000000000000000000 ) ) ;
#134297=LINE ( 'NONE', #154, #106582 ) ;
#134299=ORIENTED_EDGE ( 'NONE', *, *, #47265, .T. ) ;
#134300=EDGE_CURVE ( 'NONE', #127633, #129923, #90213, .T. ) ;
#134301=PLANE ( 'NONE',  #139076 ) ;
#134302=CARTESIAN_POINT ( 'NONE',  ( -6.707013264292997157, -21.74070752338405654, 4.999753212805220670 ) ) ;
#134303=PLANE ( 'NONE',  #123654 ) ;
#134304=VECTOR ( 'NONE', #65692, 1000.000000000000000 ) ;
#134305=DIRECTION ( 'NONE',  ( -0.3543493200069162685, -0.000000000000000000, -0.9351131265310288487 ) ) ;
#134306=CARTESIAN_POINT ( 'NONE',  ( -3.183988606268992161, 28.73617430169789699, 5.000000000000000000 ) ) ;
#134307=DIRECTION ( 'NONE',  ( 0.000000000000000000, -1.000000000000000000, 0.000000000000000000 ) ) ;
#134308=CARTESIAN_POINT ( 'NONE',  ( 27.29974487139158512, -27.71228299555225405, 4.000000000000000000 ) ) ;
#134310=DIRECTION ( 'NONE',  ( -0.7071067811865487940, 0.7071067811865463515, -0.000000000000000000 ) ) ;
#134311=PLANE ( 'NONE',  #122493 ) ;
#134313=EDGE_LOOP ( 'NONE', ( #107731, #111794, #137502, #88910 ) ) ;
#134315=CARTESIAN_POINT ( 'NONE',  ( -24.18398860626899705, 28.73617430169804265, 5.000000000000000000 ) ) ;
#134316=VECTOR ( 'NONE', #6565, 999.9999999999998863 ) ;
#134317=VECTOR ( 'NONE', #56428, 999.9999999999998863 ) ;
#134320=ADVANCED_FACE ( 'NONE', ( #93453 ), #83292, .F. ) ;
#134324=ORIENTED_EDGE ( 'NONE', *, *, #3261, .T. ) ;
#134325=VECTOR ( 'NONE', #76534, 1000.000000000000000 ) ;
#134326=CARTESIAN_POINT ( 'NONE',  ( -8.576721541936407789, 11.25929247661560240, 17.85071094206586650 ) ) ;
#134327=ORIENTED_EDGE ( 'NONE', *, *, #138389, .T. ) ;
#134328=LINE ( 'NONE', #125605, #84344 ) ;
#134329=AXIS2_PLACEMENT_3D ( 'NONE', #38373, #27466, #71729 ) ;
#134331=CARTESIAN_POINT ( 'NONE',  ( -32.67183060077624646, 5.259292476615669010, 4.000000000000000000 ) ) ;
#134332=PLANE ( 'NONE',  #81235 ) ;
#134333=ORIENTED_EDGE ( 'NONE', *, *, #41060, .T. ) ;
#134334=LINE ( 'NONE', #124156, #83628 ) ;
#134335=ORIENTED_EDGE ( 'NONE', *, *, #56610, .F. ) ;
#134336=VECTOR ( 'NONE', #73635, 1000.000000000000000 ) ;
#134338=CARTESIAN_POINT ( 'NONE',  ( -9.489213562373095101, -27.52281430457062328, 5.000000000000000000 ) ) ;
#134339=PLANE ( 'NONE',  #46948 ) ;
#134340=AXIS2_PLACEMENT_3D ( 'NONE', #12509, #79256, #24120 ) ;
#134341=DIRECTION ( 'NONE',  ( -0.3543493200069162685, -0.000000000000000000, -0.9351131265310288487 ) ) ;
#134343=EDGE_CURVE ( 'NONE', #68198, #127842, #103341, .T. ) ;
#134344=ORIENTED_EDGE ( 'NONE', *, *, #37440, .T. ) ;
#134348=EDGE_CURVE ( 'NONE', #113319, #60930, #82576, .T. ) ;
#134349=FACE_OUTER_BOUND ( 'NONE', #65449, .T. ) ;
#134350=FACE_OUTER_BOUND ( 'NONE', #88714, .T. ) ;
#134351=ADVANCED_FACE ( 'NONE', ( #64387 ), #119451, .F. ) ;
#134352=LINE ( 'NONE', #35049, #52531 ) ;
#134353=VERTEX_POINT ( 'NONE', #20865 ) ;
#134354=ORIENTED_EDGE ( 'NONE', *, *, #7143, .T. ) ;
#134355=VECTOR ( 'NONE', #138573, 1000.000000000000000 ) ;
#134356=LINE ( 'NONE', #24857, #139636 ) ;
#134357=ORIENTED_EDGE ( 'NONE', *, *, #90866, .T. ) ;
#134358=ADVANCED_FACE ( 'NONE', ( #131794 ), #22982, .F. ) ;
#134359=CARTESIAN_POINT ( 'NONE',  ( 7.499999999999947597, 6.431123077392115306, 4.000000000000000000 ) ) ;
#134361=FACE_OUTER_BOUND ( 'NONE', #82334, .T. ) ;
#134362=LINE ( 'NONE', #45236, #57233 ) ;
#134363=VECTOR ( 'NONE', #134059, 1000.000000000000000 ) ;
#134365=ADVANCED_FACE ( 'NONE', ( #65863 ), #9239, .F. ) ;
#134366=FACE_BOUND ( 'NONE', #71134, .T. ) ;
#134368=DIRECTION ( 'NONE',  ( -0.000000000000000000, 0.3543493200069153248, 0.9351131265310292928 ) ) ;
#134369=PLANE ( 'NONE',  #90714 ) ;
#134370=PLANE ( 'NONE',  #13198 ) ;
#134371=DIRECTION ( 'NONE',  ( 1.000000000000000000, 0.000000000000000000, 0.000000000000000000 ) ) ;
#134372=ORIENTED_EDGE ( 'NONE', *, *, #121401, .F. ) ;
#134374=CARTESIAN_POINT ( 'NONE',  ( 34.92499999999998295, -5.337538124160927211, 4.000000000000000000 ) ) ;
#134375=EDGE_CURVE ( 'NONE', #38197, #81300, #21602, .T. ) ;
#134376=ORIENTED_EDGE ( 'NONE', *, *, #4194, .F. ) ;
#134380=LINE ( 'NONE', #46704, #139072 ) ;
#134381=VERTEX_POINT ( 'NONE', #32484 ) ;
#134382=CARTESIAN_POINT ( 'NONE',  ( 33.70710678118631165, -18.74070752338409562, 5.000000000000000000 ) ) ;
#134384=AXIS2_PLACEMENT_3D ( 'NONE', #98417, #46211, #9963 ) ;
#134385=CARTESIAN_POINT ( 'NONE',  ( 14.81601139373099585, 28.73617430169776910, 5.000000000000000000 ) ) ;
#134386=AXIS2_PLACEMENT_3D ( 'NONE', #87262, #19144, #30008 ) ;
#134387=CARTESIAN_POINT ( 'NONE',  ( -31.64175702458840789, 15.75929247661556332, 19.34181609438707383 ) ) ;
#134389=PLANE ( 'NONE',  #1785 ) ;
#134390=CARTESIAN_POINT ( 'NONE',  ( -3.693269933095963964, -3.740707523384241728, 12.88036043432868460 ) ) ;
#134391=CARTESIAN_POINT ( 'NONE',  ( -5.999999999999960032, -15.41253812416059432, 4.000000000000000000 ) ) ;
#134392=ORIENTED_EDGE ( 'NONE', *, *, #80877, .T. ) ;
#134393=ADVANCED_FACE ( 'NONE', ( #96968 ), #42665, .F. ) ;
#134394=VECTOR ( 'NONE', #26003, 1000.000000000000000 ) ;
#134396=VECTOR ( 'NONE', #59387, 1000.000000000000227 ) ;
#134398=DIRECTION ( 'NONE',  ( -0.7071067811865487940, 0.7071067811865463515, 0.000000000000000000 ) ) ;
#134399=CARTESIAN_POINT ( 'NONE',  ( 6.707013264292989163, -21.74070752338407075, 4.999753212805213565 ) ) ;
#134402=ORIENTED_EDGE ( 'NONE', *, *, #38277, .T. ) ;
#134403=ORIENTED_EDGE ( 'NONE', *, *, #80475, .F. ) ;
#134405=EDGE_LOOP ( 'NONE', ( #35251, #112455, #67258, #75008 ) ) ;
#134407=CARTESIAN_POINT ( 'NONE',  ( -27.70710678118633652, -12.74070752338415247, 5.000000000000000000 ) ) ;
#134408=EDGE_CURVE ( 'NONE', #139225, #98928, #142666, .T. ) ;
#134410=CARTESIAN_POINT ( 'NONE',  ( 34.92499999999998295, 2.464645009310418633, -2.487937186831653325 ) ) ;
#134411=ORIENTED_EDGE ( 'NONE', *, *, #119747, .T. ) ;
#134412=CARTESIAN_POINT ( 'NONE',  ( -34.92500000000001137, 22.22500000000000142, 4.000000000000000000 ) ) ;
#134415=CARTESIAN_POINT ( 'NONE',  ( -9.005480084712511157, 28.92564299267931816, 4.000000000000000000 ) ) ;
#134416=CARTESIAN_POINT ( 'NONE',  ( 72.48921356237309510, -27.52281430457106026, 5.000000000000000000 ) ) ;
#134417=ORIENTED_EDGE ( 'NONE', *, *, #10733, .F. ) ;
#134418=ORIENTED_EDGE ( 'NONE', *, *, #2361, .F. ) ;
#134420=CARTESIAN_POINT ( 'NONE',  ( -33.49816348513935793, -17.24070752338410628, 8.407044977365300653 ) ) ;
#134421=CARTESIAN_POINT ( 'NONE',  ( -45.48921356237309510, -27.52281430457087197, 5.000000000000000000 ) ) ;
#134422=ORIENTED_EDGE ( 'NONE', *, *, #103479, .T. ) ;
#134423=VECTOR ( 'NONE', #40042, 1000.000000000000227 ) ;
#134424=DIRECTION ( 'NONE',  ( -0.6830127018922181881, 0.6830127018922202975, -0.2588190451025214056 ) ) ;
#134425=FACE_OUTER_BOUND ( 'NONE', #124015, .T. ) ;
#134426=AXIS2_PLACEMENT_3D ( 'NONE', #142237, #32758, #87120 ) ;
#134428=VECTOR ( 'NONE', #66191, 1000.000000000000000 ) ;
#134429=DIRECTION ( 'NONE',  ( 0.7071067811865487940, -0.7071067811865463515, 0.000000000000000000 ) ) ;
#134430=PLANE ( 'NONE',  #72600 ) ;
#134432=AXIS2_PLACEMENT_3D ( 'NONE', #49609, #50300, #16190 ) ;
#134433=CARTESIAN_POINT ( 'NONE',  ( -21.81246187583931473, -22.22500000000000142, 4.000000000000000000 ) ) ;
#134434=PLANE ( 'NONE',  #16689 ) ;
#134435=DIRECTION ( 'NONE',  ( 0.7071067811865487940, 0.7071067811865463515, 0.000000000000000000 ) ) ;
#134436=CARTESIAN_POINT ( 'NONE',  ( -16.49999999999989697, -14.70932175296479549, -11.46312253303834261 ) ) ;
#134437=VERTEX_POINT ( 'NONE', #53520 ) ;
#134438=EDGE_CURVE ( 'NONE', #93683, #26697, #20148, .T. ) ;
#134439=VECTOR ( 'NONE', #122845, 1000.000000000000000 ) ;
#134440=VERTEX_POINT ( 'NONE', #97726 ) ;
#134442=CARTESIAN_POINT ( 'NONE',  ( 32.99999999999977263, -19.06887692260762179, 4.000000000000000000 ) ) ;
#134443=LINE ( 'NONE', #124974, #29673 ) ;
#134444=ORIENTED_EDGE ( 'NONE', *, *, #87535, .F. ) ;
#134445=VECTOR ( 'NONE', #42471, 1000.000000000000000 ) ;
#134446=LINE ( 'NONE', #24935, #108570 ) ;
#134447=DIRECTION ( 'NONE',  ( -0.6830127018922181881, 0.6830127018922202975, -0.2588190451025214056 ) ) ;
#134448=DIRECTION ( 'NONE',  ( -0.000000000000000000, 0.3543493200069153248, 0.9351131265310292928 ) ) ;
#134449=ORIENTED_EDGE ( 'NONE', *, *, #60379, .F. ) ;
#134450=DIRECTION ( 'NONE',  ( -0.000000000000000000, 0.000000000000000000, 1.000000000000000000 ) ) ;
#134451=VECTOR ( 'NONE', #110899, 1000.000000000000000 ) ;
#134452=CARTESIAN_POINT ( 'NONE',  ( 35.99451991528749772, 28.92564299267963079, 4.000000000000000000 ) ) ;
#134453=CARTESIAN_POINT ( 'NONE',  ( 29.99999999999979039, 15.45873954670187445, -0.03131636524301203289 ) ) ;
#134455=DIRECTION ( 'NONE',  ( -0.3543493200069162685, -0.000000000000000000, -0.9351131265310288487 ) ) ;
#134457=PLANE ( 'NONE',  #27881 ) ;
#134458=EDGE_CURVE ( 'NONE', #60511, #109568, #534, .T. ) ;
#134459=ORIENTED_EDGE ( 'NONE', *, *, #1875, .T. ) ;
#134461=EDGE_LOOP ( 'NONE', ( #32245, #77166, #134622, #100130 ) ) ;
#134462=VECTOR ( 'NONE', #61676, 999.9999999999998863 ) ;
#134463=CARTESIAN_POINT ( 'NONE',  ( -30.48921356237309510, -27.52281430457076894, 5.000000000000000000 ) ) ;
#134465=DIRECTION ( 'NONE',  ( -0.6830127018922180770, -0.6830127018922204085, -0.2588190451025213501 ) ) ;
#134466=CARTESIAN_POINT ( 'NONE',  ( -3.489213562373097322, -27.52281430457057709, 5.000000000000000000 ) ) ;
#134467=ADVANCED_FACE ( 'NONE', ( #65129 ), #99123, .F. ) ;
#134468=CARTESIAN_POINT ( 'NONE',  ( 0.000000000000000000, 0.000000000000000000, 5.000000000000000000 ) ) ;
#134469=CARTESIAN_POINT ( 'NONE',  ( 48.18398860626899705, 28.73617430169820608, 5.000000000000000000 ) ) ;
#134470=ORIENTED_EDGE ( 'NONE', *, *, #12421, .T. ) ;
#134471=ADVANCED_FACE ( 'NONE', ( #89020 ), #33916, .F. ) ;
#134472=ORIENTED_EDGE ( 'NONE', *, *, #49133, .T. ) ;
#134473=LINE ( 'NONE', #79420, #57977 ) ;
#134474=CARTESIAN_POINT ( 'NONE',  ( -24.48921356237309510, -27.52281430457072631, 5.000000000000000000 ) ) ;
#134477=AXIS2_PLACEMENT_3D ( 'NONE', #23118, #134073, #10824 ) ;
#134478=CARTESIAN_POINT ( 'NONE',  ( 11.99451991528749417, 28.92564299267946382, 4.000000000000000000 ) ) ;
#134481=FACE_OUTER_BOUND ( 'NONE', #67141, .T. ) ;
#134482=DIRECTION ( 'NONE',  ( -0.7071067811865486830, 0.7071067811865464625, 0.000000000000000000 ) ) ;
#134483=VERTEX_POINT ( 'NONE', #132544 ) ;
#134485=LINE ( 'NONE', #20699, #141905 ) ;
#134486=DIRECTION ( 'NONE',  ( -0.7071067811865486830, 0.7071067811865464625, 0.000000000000000000 ) ) ;
#134488=EDGE_LOOP ( 'NONE', ( #118301, #107957, #80581, #128346 ) ) ;
#134489=VECTOR ( 'NONE', #62073, 1000.000000000000000 ) ;
#134490=ADVANCED_FACE ( 'NONE', ( #43359 ), #87571, .T. ) ;
#134492=AXIS2_PLACEMENT_3D ( 'NONE', #114389, #136139, #36824 ) ;
#134493=VECTOR ( 'NONE', #80343, 1000.000000000000000 ) ;
#134496=ORIENTED_EDGE ( 'NONE', *, *, #8699, .T. ) ;
#134497=VECTOR ( 'NONE', #120461, 1000.000000000000000 ) ;
#134498=ORIENTED_EDGE ( 'NONE', *, *, #9905, .T. ) ;
#134499=VECTOR ( 'NONE', #7276, 1000.000000000000000 ) ;
#134500=VECTOR ( 'NONE', #83517, 999.9999999999998863 ) ;
#134503=DIRECTION ( 'NONE',  ( 0.7071067811865487940, 0.7071067811865463515, -0.000000000000000000 ) ) ;
#134505=CARTESIAN_POINT ( 'NONE',  ( -34.82816939922327748, 12.75929247661559529, 4.000000000000000000 ) ) ;
#134506=PLANE ( 'NONE',  #45315 ) ;
#134508=PLANE ( 'NONE',  #2008 ) ;
#134509=CARTESIAN_POINT ( 'NONE',  ( 2.241399257802041856, 21.72499999999999432, 5.000000000000000000 ) ) ;
#134510=FACE_OUTER_BOUND ( 'NONE', #49114, .T. ) ;
#134511=VECTOR ( 'NONE', #38915, 1000.000000000000000 ) ;
#134512=DIRECTION ( 'NONE',  ( 0.6830127018922181881, 0.6830127018922202975, -0.2588190451025214056 ) ) ;
#134513=ORIENTED_EDGE ( 'NONE', *, *, #134014, .T. ) ;
#134514=VERTEX_POINT ( 'NONE', #125195 ) ;
#134515=EDGE_CURVE ( 'NONE', #36084, #106881, #91840, .T. ) ;
#134517=EDGE_CURVE ( 'NONE', #98656, #128903, #80288, .T. ) ;
#134518=ORIENTED_EDGE ( 'NONE', *, *, #132574, .F. ) ;
#134519=AXIS2_PLACEMENT_3D ( 'NONE', #39879, #49332, #93516 ) ;
#134520=CARTESIAN_POINT ( 'NONE',  ( 24.48921356237309510, -27.52281430457072631, 5.000000000000000000 ) ) ;
#134521=ADVANCED_FACE ( 'NONE', ( #136065 ), #70151, .F. ) ;
#134522=DIRECTION ( 'NONE',  ( 0.7071067811865487940, 0.7071067811865463515, -0.000000000000000000 ) ) ;
#134523=DIRECTION ( 'NONE',  ( -1.000000000000000000, 0.000000000000000000, 0.000000000000000000 ) ) ;
#134524=VECTOR ( 'NONE', #54070, 999.9999999999998863 ) ;
#134528=VERTEX_POINT ( 'NONE', #1243 ) ;
#134529=DIRECTION ( 'NONE',  ( -0.6830127018922180770, -0.6830127018922204085, -0.2588190451025213501 ) ) ;
#134532=EDGE_CURVE ( 'NONE', #53505, #24661, #80988, .T. ) ;
#134533=ORIENTED_EDGE ( 'NONE', *, *, #110546, .F. ) ;
#134534=VECTOR ( 'NONE', #46655, 1000.000000000000227 ) ;
#134537=CARTESIAN_POINT ( 'NONE',  ( -34.75611968250420603, -6.187065745292570362, 4.955485411084898040 ) ) ;
#134538=CARTESIAN_POINT ( 'NONE',  ( 0.000000000000000000, 0.000000000000000000, 5.000000000000000000 ) ) ;
#134539=VECTOR ( 'NONE', #123247, 1000.000000000000000 ) ;
#134541=ADVANCED_FACE ( 'NONE', ( #113588 ), #14988, .F. ) ;
#134542=FACE_BOUND ( 'NONE', #29699, .T. ) ;
#134544=EDGE_CURVE ( 'NONE', #5991, #126851, #59262, .T. ) ;
#134546=CARTESIAN_POINT ( 'NONE',  ( -34.92500000000001137, 22.22500000000000142, 4.000000000000000000 ) ) ;
#134548=CARTESIAN_POINT ( 'NONE',  ( 32.99999999999975842, -13.39766691384881092, -10.96608748226473828 ) ) ;
#134550=ORIENTED_EDGE ( 'NONE', *, *, #142496, .F. ) ;
#134552=ORIENTED_EDGE ( 'NONE', *, *, #39841, .T. ) ;
#134554=ORIENTED_EDGE ( 'NONE', *, *, #88654, .T. ) ;
#134555=EDGE_CURVE ( 'NONE', #80319, #51865, #134712, .T. ) ;
#134556=PLANE ( 'NONE',  #102122 ) ;
#134557=VERTEX_POINT ( 'NONE', #12134 ) ;
#134558=VECTOR ( 'NONE', #49097, 999.9999999999998863 ) ;
#134560=EDGE_CURVE ( 'NONE', #22767, #51759, #46979, .T. ) ;
#134561=VECTOR ( 'NONE', #105360, 1000.000000000000227 ) ;
#134563=DIRECTION ( 'NONE',  ( 0.3543493200069162685, -0.000000000000000000, -0.9351131265310288487 ) ) ;
#134564=VERTEX_POINT ( 'NONE', #89705 ) ;
#134565=CARTESIAN_POINT ( 'NONE',  ( -28.49999999999979750, -6.839392718269155402, -8.480912228396016772 ) ) ;
#134566=DIRECTION ( 'NONE',  ( -0.7071067811865486830, -0.7071067811865464625, 0.000000000000000000 ) ) ;
#134569=PLANE ( 'NONE',  #41179 ) ;
#134572=VECTOR ( 'NONE', #4722, 1000.000000000000000 ) ;
#134574=ORIENTED_EDGE ( 'NONE', *, *, #21206, .F. ) ;
#134575=LINE ( 'NONE', #78048, #135238 ) ;
#134576=CARTESIAN_POINT ( 'NONE',  ( -25.01459476339044130, 2.945717840782780428, 4.000000000000000000 ) ) ;
#134577=ORIENTED_EDGE ( 'NONE', *, *, #4457, .T. ) ;
#134579=ORIENTED_EDGE ( 'NONE', *, *, #68273, .F. ) ;
#134580=EDGE_CURVE ( 'NONE', #106170, #135404, #68009, .T. ) ;
#134582=EDGE_CURVE ( 'NONE', #130556, #17773, #47679, .T. ) ;
#134584=ORIENTED_EDGE ( 'NONE', *, *, #99160, .F. ) ;
#134585=PLANE ( 'NONE',  #136999 ) ;
#134586=EDGE_CURVE ( 'NONE', #140292, #94283, #90421, .T. ) ;
#134589=LINE ( 'NONE', #12763, #54094 ) ;
#134590=ORIENTED_EDGE ( 'NONE', *, *, #60958, .T. ) ;
#134591=CARTESIAN_POINT ( 'NONE',  ( 33.18398860626899705, 28.73617430169810305, 5.000000000000000000 ) ) ;
#134592=ORIENTED_EDGE ( 'NONE', *, *, #116602, .F. ) ;
#134593=DIRECTION ( 'NONE',  ( 0.7071067811865487940, -0.7071067811865463515, 0.000000000000000000 ) ) ;
#134594=CARTESIAN_POINT ( 'NONE',  ( 30.79289321881324781, 6.759292476615653023, 5.000000000000000000 ) ) ;
#134595=ORIENTED_EDGE ( 'NONE', *, *, #18487, .T. ) ;
#134596=CARTESIAN_POINT ( 'NONE',  ( -5.510786437626906675, -27.52281430457051314, 5.000000000000000000 ) ) ;
#134598=CIRCLE ( 'NONE', #88339, 5.968999999999998529 ) ;
#134599=ORIENTED_EDGE ( 'NONE', *, *, #74114, .F. ) ;
#134600=DIRECTION ( 'NONE',  ( -0.6830127018922181881, 0.6830127018922202975, -0.2588190451025214056 ) ) ;
#134601=ORIENTED_EDGE ( 'NONE', *, *, #89612, .F. ) ;
#134603=ORIENTED_EDGE ( 'NONE', *, *, #45738, .F. ) ;
#134604=VECTOR ( 'NONE', #104450, 1000.000000000000000 ) ;
#134605=VECTOR ( 'NONE', #58378, 1000.000000000000227 ) ;
#134606=VECTOR ( 'NONE', #28895, 1000.000000000000000 ) ;
#134607=VECTOR ( 'NONE', #112395, 1000.000000000000000 ) ;
#134609=DIRECTION ( 'NONE',  ( 0.7071067811865486830, -0.7071067811865464625, -0.000000000000000000 ) ) ;
#134610=PLANE ( 'NONE',  #75153 ) ;
#134611=DIRECTION ( 'NONE',  ( 0.7071067811865487940, 0.7071067811865463515, 0.000000000000000000 ) ) ;
#134612=DIRECTION ( 'NONE',  ( -0.3543493200069162685, -0.000000000000000000, -0.9351131265310288487 ) ) ;
#134613=VECTOR ( 'NONE', #85094, 1000.000000000000000 ) ;
#134614=VERTEX_POINT ( 'NONE', #106092 ) ;
#134615=FACE_OUTER_BOUND ( 'NONE', #13395, .T. ) ;
#134617=DIRECTION ( 'NONE',  ( -0.000000000000000000, 0.3543493200069153248, 0.9351131265310292928 ) ) ;
#134618=CARTESIAN_POINT ( 'NONE',  ( 22.49999999999984368, -17.91344420646040447, 1.358650452708515921 ) ) ;
#134619=AXIS2_PLACEMENT_3D ( 'NONE', #115583, #96697, #16285 ) ;
#134621=VERTEX_POINT ( 'NONE', #18369 ) ;
#134622=ORIENTED_EDGE ( 'NONE', *, *, #9053, .F. ) ;
#134624=ORIENTED_EDGE ( 'NONE', *, *, #106568, .T. ) ;
#134626=CARTESIAN_POINT ( 'NONE',  ( -29.99999999999979039, -6.033600742197676503, 5.000000000000000000 ) ) ;
#134628=PLANE ( 'NONE',  #979 ) ;
#134631=VECTOR ( 'NONE', #110089, 1000.000000000000000 ) ;
#134632=VECTOR ( 'NONE', #142015, 1000.000000000000000 ) ;
#134633=CARTESIAN_POINT ( 'NONE',  ( -2.292893218813429890, 11.25929247661560417, 5.000000000000000000 ) ) ;
#134634=DIRECTION ( 'NONE',  ( 0.7071067811865487940, 0.7071067811865463515, 0.000000000000000000 ) ) ;
#134635=FACE_OUTER_BOUND ( 'NONE', #80664, .T. ) ;
#134636=DIRECTION ( 'NONE',  ( -0.000000000000000000, 0.3543493200069153248, 0.9351131265310292928 ) ) ;
#134637=VECTOR ( 'NONE', #94434, 1000.000000000000000 ) ;
#134638=DIRECTION ( 'NONE',  ( 1.000000000000000000, 0.000000000000000000, 0.000000000000000000 ) ) ;
#134639=ORIENTED_EDGE ( 'NONE', *, *, #8258, .F. ) ;
#134640=VECTOR ( 'NONE', #56416, 1000.000000000000227 ) ;
#134641=VERTEX_POINT ( 'NONE', #40199 ) ;
#134643=ORIENTED_EDGE ( 'NONE', *, *, #74648, .T. ) ;
#134644=EDGE_CURVE ( 'NONE', #6354, #55705, #108228, .T. ) ;
#134645=AXIS2_PLACEMENT_3D ( 'NONE', #87897, #129983, #132141 ) ;
#134647=CARTESIAN_POINT ( 'NONE',  ( -0.2997448713915885632, -27.71228299555206220, 4.000000000000000000 ) ) ;
#134648=ORIENTED_EDGE ( 'NONE', *, *, #66746, .T. ) ;
#134651=ORIENTED_EDGE ( 'NONE', *, *, #65583, .T. ) ;
#134652=CARTESIAN_POINT ( 'NONE',  ( -12.48921356237309155, -27.52281430457064104, 5.000000000000000000 ) ) ;
#134653=ORIENTED_EDGE ( 'NONE', *, *, #119431, .T. ) ;
#134654=EDGE_CURVE ( 'NONE', #113899, #82267, #6766, .T. ) ;
#134655=CARTESIAN_POINT ( 'NONE',  ( 39.48921356237310221, -27.52281430457082934, 5.000000000000000000 ) ) ;
#134658=CARTESIAN_POINT ( 'NONE',  ( 32.99999999999976552, 20.58746187583904330, 4.000000000000000000 ) ) ;
#134660=EDGE_CURVE ( 'NONE', #142281, #61677, #30736, .T. ) ;
#134661=PLANE ( 'NONE',  #12094 ) ;
#134662=CARTESIAN_POINT ( 'NONE',  ( -20.20666063542138957, 21.75929247661549226, 4.998822639870715179 ) ) ;
#134665=VECTOR ( 'NONE', #133437, 1000.000000000000000 ) ;
#134666=CARTESIAN_POINT ( 'NONE',  ( -69.29974487139159578, -27.71228299555254537, 4.000000000000000000 ) ) ;
#134667=FACE_OUTER_BOUND ( 'NONE', #125534, .T. ) ;
#134669=CARTESIAN_POINT ( 'NONE',  ( -29.28242261357413057, -21.73023691814492864, 5.000000000000000888 ) ) ;
#134672=PLANE ( 'NONE',  #83704 ) ;
#134673=ORIENTED_EDGE ( 'NONE', *, *, #102397, .F. ) ;
#134675=VECTOR ( 'NONE', #35465, 1000.000000000000000 ) ;
#134676=LINE ( 'NONE', #35372, #124103 ) ;
#134679=AXIS2_PLACEMENT_3D ( 'NONE', #49752, #73621, #29381 ) ;
#134680=DIRECTION ( 'NONE',  ( -0.3543493200069163240, -0.000000000000000000, 0.9351131265310288487 ) ) ;
#134681=ORIENTED_EDGE ( 'NONE', *, *, #48661, .T. ) ;
#134682=EDGE_CURVE ( 'NONE', #124216, #72242, #56826, .T. ) ;
#134683=DIRECTION ( 'NONE',  ( -0.000000000000000000, 0.000000000000000000, 1.000000000000000000 ) ) ;
#134685=DIRECTION ( 'NONE',  ( -0.6830127018922180770, -0.6830127018922204085, -0.2588190451025213501 ) ) ;
#134687=DIRECTION ( 'NONE',  ( 0.7071067811865486830, -0.7071067811865464625, -0.000000000000000000 ) ) ;
#134688=FACE_OUTER_BOUND ( 'NONE', #103189, .T. ) ;
#134689=VERTEX_POINT ( 'NONE', #127909 ) ;
#134690=DIRECTION ( 'NONE',  ( 0.7071067811865487940, 0.7071067811865463515, 0.000000000000000000 ) ) ;
#134691=ADVANCED_FACE ( 'NONE', ( #28589 ), #118418, .F. ) ;
#134692=FACE_OUTER_BOUND ( 'NONE', #1766, .T. ) ;
#134693=AXIS2_PLACEMENT_3D ( 'NONE', #126935, #50832, #139292 ) ;
#134694=CARTESIAN_POINT ( 'NONE',  ( 2.510786437626908008, -27.52281430457053446, 5.000000000000000000 ) ) ;
#134695=PLANE ( 'NONE',  #8521 ) ;
#134696=DIRECTION ( 'NONE',  ( -0.7071067811865486830, 0.7071067811865464625, 0.000000000000000000 ) ) ;
#134697=ORIENTED_EDGE ( 'NONE', *, *, #48328, .F. ) ;
#134698=ORIENTED_EDGE ( 'NONE', *, *, #125199, .T. ) ;
#134699=EDGE_LOOP ( 'NONE', ( #86383, #32668, #80161, #20717 ) ) ;
#134701=ORIENTED_EDGE ( 'NONE', *, *, #72994, .F. ) ;
#134702=CARTESIAN_POINT ( 'NONE',  ( -34.42500000000001137, -21.72500000000000142, 4.500000000000000888 ) ) ;
#134703=EDGE_CURVE ( 'NONE', #43125, #32348, #116291, .T. ) ;
#134704=DIRECTION ( 'NONE',  ( 0.3543493200069162685, -0.000000000000000000, -0.9351131265310288487 ) ) ;
#134705=PLANE ( 'NONE',  #78134 ) ;
#134706=DIRECTION ( 'NONE',  ( -0.7071067811865486830, 0.7071067811865464625, 0.000000000000000000 ) ) ;
#134707=ORIENTED_EDGE ( 'NONE', *, *, #9409, .F. ) ;
#134709=VECTOR ( 'NONE', #106550, 1000.000000000000000 ) ;
#134710=LINE ( 'NONE', #15702, #28264 ) ;
#134711=FACE_OUTER_BOUND ( 'NONE', #77698, .T. ) ;
#134712=( BOUNDED_CURVE ( )  B_SPLINE_CURVE ( 3, ( #2680, #35363, #134669, #1934 ),
 .UNSPECIFIED., .F., .F. ) 
 B_SPLINE_CURVE_WITH_KNOTS ( ( 4, 4 ),
 ( 1.901594255663634492, 1.933014472006554740 ),
 .UNSPECIFIED. ) 
 CURVE ( )  GEOMETRIC_REPRESENTATION_ITEM ( )  RATIONAL_B_SPLINE_CURVE ( ( 1.000000000000000000, 0.9999177325257868620, 0.9999177325257868620, 1.000000000000000000 ) ) 
 REPRESENTATION_ITEM ( '' )  );
#134713=EDGE_CURVE ( 'NONE', #107902, #45966, #105403, .T. ) ;
#134716=VECTOR ( 'NONE', #90123, 1000.000000000000000 ) ;
#134718=ORIENTED_EDGE ( 'NONE', *, *, #11788, .T. ) ;
#134719=CARTESIAN_POINT ( 'NONE',  ( 15.63964197871511885, 8.074661077379714058, 4.334728602384618767 ) ) ;
#134720=AXIS2_PLACEMENT_3D ( 'NONE', #120123, #65094, #122278 ) ;
#134721=VECTOR ( 'NONE', #120903, 999.9999999999998863 ) ;
#134723=VECTOR ( 'NONE', #115684, 1000.000000000000000 ) ;
#134724=VECTOR ( 'NONE', #112229, 1000.000000000000000 ) ;
#134725=EDGE_CURVE ( 'NONE', #76657, #136607, #29984, .T. ) ;
#134726=VECTOR ( 'NONE', #94225, 999.9999999999998863 ) ;
#134727=ORIENTED_EDGE ( 'NONE', *, *, #55483, .F. ) ;
#134728=ORIENTED_EDGE ( 'NONE', *, *, #60211, .T. ) ;
#134729=DIRECTION ( 'NONE',  ( 0.3543493200069162685, -0.000000000000000000, -0.9351131265310288487 ) ) ;
#134730=EDGE_CURVE ( 'NONE', #18576, #32728, #72847, .T. ) ;
#134731=CARTESIAN_POINT ( 'NONE',  ( -7.786780966966368567, 12.75929247661558996, 10.29404684609033538 ) ) ;
#134733=PLANE ( 'NONE',  #122057 ) ;
#134734=CARTESIAN_POINT ( 'NONE',  ( -23.67183060077630685, 17.25929247661554200, 4.000000000000000000 ) ) ;
#134736=ORIENTED_EDGE ( 'NONE', *, *, #143484, .T. ) ;
#134738=EDGE_CURVE ( 'NONE', #82163, #126053, #51048, .T. ) ;
#134739=FACE_OUTER_BOUND ( 'NONE', #44353, .T. ) ;
#134741=ORIENTED_EDGE ( 'NONE', *, *, #131495, .F. ) ;
#134742=EDGE_CURVE ( 'NONE', #37853, #28081, #139515, .T. ) ;
#134744=VECTOR ( 'NONE', #8930, 1000.000000000000000 ) ;
#134745=DIRECTION ( 'NONE',  ( -0.000000000000000000, -1.000000000000000000, -0.000000000000000000 ) ) ;
#134746=ORIENTED_EDGE ( 'NONE', *, *, #3836, .T. ) ;
#134747=CARTESIAN_POINT ( 'NONE',  ( -5.816011393731002066, 28.73617430169783304, 5.000000000000000000 ) ) ;
#134748=FACE_OUTER_BOUND ( 'NONE', #10206, .T. ) ;
#134749=VECTOR ( 'NONE', #129570, 1000.000000000000000 ) ;
#134750=LINE ( 'NONE', #81066, #119734 ) ;
#134751=LINE ( 'NONE', #35444, #57730 ) ;
#134752=VECTOR ( 'NONE', #113239, 999.9999999999998863 ) ;
#134753=DIRECTION ( 'NONE',  ( -0.7071067811865486830, 0.7071067811865464625, 0.000000000000000000 ) ) ;
#134754=ORIENTED_EDGE ( 'NONE', *, *, #53359, .F. ) ;
#134755=CARTESIAN_POINT ( 'NONE',  ( -34.76445279868696758, 22.22500000000000142, 5.060837336147055332 ) ) ;
#134756=ORIENTED_EDGE ( 'NONE', *, *, #16138, .F. ) ;
#134757=LINE ( 'NONE', #78215, #78223 ) ;
#134758=ORIENTED_EDGE ( 'NONE', *, *, #125024, .T. ) ;
#134759=CARTESIAN_POINT ( 'NONE',  ( -63.18398860626900415, 28.73617430169831621, 5.000000000000000000 ) ) ;
#134760=ORIENTED_EDGE ( 'NONE', *, *, #37958, .F. ) ;
#134761=PLANE ( 'NONE',  #115307 ) ;
#134762=ORIENTED_EDGE ( 'NONE', *, *, #68214, .F. ) ;
#134763=EDGE_LOOP ( 'NONE', ( #64908, #53614, #132224, #14671 ) ) ;
#134764=AXIS2_PLACEMENT_3D ( 'NONE', #27740, #93722, #71999 ) ;
#134765=ORIENTED_EDGE ( 'NONE', *, *, #108715, .F. ) ;
#134766=ADVANCED_FACE ( 'NONE', ( #128602 ), #29276, .F. ) ;
#134767=CARTESIAN_POINT ( 'NONE',  ( 23.96628934044694148, -0.2106608083017111055, 4.443784815937100063 ) ) ;
#134771=CARTESIAN_POINT ( 'NONE',  ( -28.49999999999979750, -9.462702396501040170, -9.474982329943451020 ) ) ;
#134772=LINE ( 'NONE', #36842, #18080 ) ;
#134773=AXIS2_PLACEMENT_3D ( 'NONE', #83333, #6412, #117347 ) ;
#134774=PLANE ( 'NONE',  #18067 ) ;
#134776=VECTOR ( 'NONE', #55661, 999.9999999999998863 ) ;
#134777=DIRECTION ( 'NONE',  ( -0.6830127018922181881, 0.6830127018922202975, -0.2588190451025214056 ) ) ;
#134779=ORIENTED_EDGE ( 'NONE', *, *, #28726, .F. ) ;
#134781=CARTESIAN_POINT ( 'NONE',  ( 34.42499999999998295, 1.541399257802028577, 5.000000000000000000 ) ) ;
#134782=LINE ( 'NONE', #134045, #26331 ) ;
#134783=ORIENTED_EDGE ( 'NONE', *, *, #103664, .T. ) ;
#134784=EDGE_LOOP ( 'NONE', ( #71091, #8536, #75228, #18562 ) ) ;
#134785=VECTOR ( 'NONE', #28347, 1000.000000000000000 ) ;
#134786=DIRECTION ( 'NONE',  ( 0.7071067811865486830, -0.7071067811865464625, -0.000000000000000000 ) ) ;
#134787=VERTEX_POINT ( 'NONE', #41577 ) ;
#134789=CARTESIAN_POINT ( 'NONE',  ( -26.29289321881327268, -0.7407075233842718154, 5.000000000000000000 ) ) ;
#134790=LINE ( 'NONE', #136178, #39394 ) ;
#134791=PLANE ( 'NONE',  #62575 ) ;
#134793=CARTESIAN_POINT ( 'NONE',  ( -21.29974487139158512, -27.71228299555221142, 4.000000000000000000 ) ) ;
#134794=VECTOR ( 'NONE', #105556, 1000.000000000000000 ) ;
#134795=ORIENTED_EDGE ( 'NONE', *, *, #57818, .F. ) ;
#134796=DIRECTION ( 'NONE',  ( 0.7071067811865486830, -0.7071067811865464625, -0.000000000000000000 ) ) ;
#134801=ORIENTED_EDGE ( 'NONE', *, *, #75860, .T. ) ;
#134802=ORIENTED_EDGE ( 'NONE', *, *, #102956, .T. ) ;
#134803=ORIENTED_EDGE ( 'NONE', *, *, #29114, .F. ) ;
#134804=LINE ( 'NONE', #71666, #68155 ) ;
#134805=CARTESIAN_POINT ( 'NONE',  ( 66.18398860626901126, 28.73617430169833753, 5.000000000000000000 ) ) ;
#134806=VECTOR ( 'NONE', #19776, 1000.000000000000000 ) ;
#134807=VECTOR ( 'NONE', #19230, 1000.000000000000000 ) ;
#134808=CARTESIAN_POINT ( 'NONE',  ( -11.51078643762690490, -27.52281430457047406, 5.000000000000000000 ) ) ;
#134809=VECTOR ( 'NONE', #18773, 999.9999999999998863 ) ;
#134810=PLANE ( 'NONE',  #119067 ) ;
#134811=ORIENTED_EDGE ( 'NONE', *, *, #138983, .F. ) ;
#134812=CARTESIAN_POINT ( 'NONE',  ( -7.171830600776418763, -5.240707523384232402, 4.000000000000000000 ) ) ;
#134815=CARTESIAN_POINT ( 'NONE',  ( 8.700255128608413102, -27.71228299555199825, 4.000000000000000000 ) ) ;
#134816=ORIENTED_EDGE ( 'NONE', *, *, #69180, .T. ) ;
#134817=VECTOR ( 'NONE', #129469, 999.9999999999998863 ) ;
#134818=AXIS2_PLACEMENT_3D ( 'NONE', #28566, #31413, #29252 ) ;
#134820=FACE_OUTER_BOUND ( 'NONE', #41135, .T. ) ;
#134821=ORIENTED_EDGE ( 'NONE', *, *, #4762, .F. ) ;
#134822=EDGE_CURVE ( 'NONE', #20530, #131775, #130030, .T. ) ;
#134824=ORIENTED_EDGE ( 'NONE', *, *, #44231, .T. ) ;
#134825=VERTEX_POINT ( 'NONE', #131464 ) ;
#134826=EDGE_CURVE ( 'NONE', #3994, #73071, #5926, .T. ) ;
#134829=CARTESIAN_POINT ( 'NONE',  ( 34.47516574401890921, -20.97193265888397207, 4.998110765256833510 ) ) ;
#134832=VERTEX_POINT ( 'NONE', #45898 ) ;
#134834=EDGE_CURVE ( 'NONE', #20599, #70176, #80917, .T. ) ;
#134836=DIRECTION ( 'NONE',  ( 0.7071067811865487940, -0.7071067811865463515, 0.000000000000000000 ) ) ;
#134837=DIRECTION ( 'NONE',  ( -0.6830127018922181881, 0.6830127018922202975, -0.2588190451025214056 ) ) ;
#134838=CARTESIAN_POINT ( 'NONE',  ( -34.92500000000001137, 11.57121408575941324, 9.037117742336748805 ) ) ;
#134839=DIRECTION ( 'NONE',  ( 0.7071067811865487940, 0.7071067811865463515, 0.000000000000000000 ) ) ;
#134840=EDGE_CURVE ( 'NONE', #103327, #68975, #33599, .T. ) ;
#134842=DIRECTION ( 'NONE',  ( 0.6830127018922181881, 0.6830127018922202975, -0.2588190451025214056 ) ) ;
#134843=LINE ( 'NONE', #114465, #64583 ) ;
#134845=FACE_OUTER_BOUND ( 'NONE', #137692, .T. ) ;
#134847=LINE ( 'NONE', #79773, #28136 ) ;
#134848=DIRECTION ( 'NONE',  ( 0.7071067811865486830, -0.7071067811865464625, -0.000000000000000000 ) ) ;
#134849=ORIENTED_EDGE ( 'NONE', *, *, #137173, .F. ) ;
#134850=VECTOR ( 'NONE', #29338, 1000.000000000000000 ) ;
#134851=ORIENTED_EDGE ( 'NONE', *, *, #134154, .F. ) ;
#134853=EDGE_CURVE ( 'NONE', #118081, #48278, #142349, .T. ) ;
#134855=ORIENTED_EDGE ( 'NONE', *, *, #52456, .T. ) ;
#134858=LINE ( 'NONE', #101468, #55002 ) ;
#134859=LINE ( 'NONE', #89875, #74180 ) ;
#134862=VERTEX_POINT ( 'NONE', #66918 ) ;
#134863=CARTESIAN_POINT ( 'NONE',  ( -36.18398860626899705, 28.73617430169812437, 5.000000000000000000 ) ) ;
#134864=CARTESIAN_POINT ( 'NONE',  ( -6.793339364578430128, 21.75929247661548871, 4.998822639870703632 ) ) ;
#134865=DIRECTION ( 'NONE',  ( -0.7071067811865486830, -0.7071067811865464625, -0.000000000000000000 ) ) ;
#134866=DIRECTION ( 'NONE',  ( 0.6830127018922180770, -0.6830127018922204085, -0.2588190451025213501 ) ) ;
#134867=CARTESIAN_POINT ( 'NONE',  ( 28.19018167574430933, -18.74070752338409207, 7.910009926591441420 ) ) ;
#134868=CARTESIAN_POINT ( 'NONE',  ( 7.499999999999954703, 1.466399257802248446, 5.000000000000000000 ) ) ;
#134869=DIRECTION ( 'NONE',  ( -0.7071067811865486830, -0.7071067811865464625, -0.000000000000000000 ) ) ;
#134870=EDGE_CURVE ( 'NONE', #138219, #5611, #916, .T. ) ;
#134871=CARTESIAN_POINT ( 'NONE',  ( 38.99451991528749062, 28.92564299267965211, 4.000000000000000000 ) ) ;
#134872=AXIS2_PLACEMENT_3D ( 'NONE', #18255, #117572, #75543 ) ;
#134873=CARTESIAN_POINT ( 'NONE',  ( 31.49999999999977973, -2.173586137069110968, -4.605770156576038055 ) ) ;
#134874=LINE ( 'NONE', #12333, #84745 ) ;
#134876=DIRECTION ( 'NONE',  ( 0.7071067811865487940, 0.7071067811865463515, -0.000000000000000000 ) ) ;
#134877=ORIENTED_EDGE ( 'NONE', *, *, #40129, .F. ) ;
#134880=( BOUNDED_CURVE ( )  B_SPLINE_CURVE ( 3, ( #142580, #44735, #65766, #43272 ),
 .UNSPECIFIED., .F., .T. ) 
 B_SPLINE_CURVE_WITH_KNOTS ( ( 4, 4 ),
 ( 5.772031613926481342, 5.830584196225661486 ),
 .UNSPECIFIED. ) 
 CURVE ( )  GEOMETRIC_REPRESENTATION_ITEM ( )  RATIONAL_B_SPLINE_CURVE ( ( 1.000000000000000000, 0.9997143199977724937, 0.9997143199977724937, 1.000000000000000000 ) ) 
 REPRESENTATION_ITEM ( '' )  );
#134881=ORIENTED_EDGE ( 'NONE', *, *, #89796, .T. ) ;
#134886=FACE_OUTER_BOUND ( 'NONE', #11492, .T. ) ;
#134890=ORIENTED_EDGE ( 'NONE', *, *, #62605, .F. ) ;
#134891=ADVANCED_FACE ( 'NONE', ( #66215 ), #55335, .F. ) ;
#134893=DIRECTION ( 'NONE',  ( 1.000000000000000000, 0.000000000000000000, 0.000000000000000000 ) ) ;
#134896=EDGE_CURVE ( 'NONE', #5082, #138480, #102427, .T. ) ;
#134898=ORIENTED_EDGE ( 'NONE', *, *, #7395, .F. ) ;
#134899=ORIENTED_EDGE ( 'NONE', *, *, #78045, .F. ) ;
#134901=AXIS2_PLACEMENT_3D ( 'NONE', #8033, #129840, #30542 ) ;
#134902=( BOUNDED_CURVE ( )  B_SPLINE_CURVE ( 3, ( #60493, #104670, #114806, #39445 ),
 .UNSPECIFIED., .F., .F. ) 
 B_SPLINE_CURVE_WITH_KNOTS ( ( 4, 4 ),
 ( 5.920967161967927161, 7.341195215986655143 ),
 .UNSPECIFIED. ) 
 CURVE ( )  GEOMETRIC_REPRESENTATION_ITEM ( )  RATIONAL_B_SPLINE_CURVE ( ( 1.000000000000000000, 0.8388583629366577199, 0.8388583629366577199, 1.000000000000000000 ) ) 
 REPRESENTATION_ITEM ( '' )  );
#134903=EDGE_CURVE ( 'NONE', #7972, #29609, #60349, .T. ) ;
#134906=ORIENTED_EDGE ( 'NONE', *, *, #98621, .T. ) ;
#134907=ADVANCED_FACE ( 'NONE', ( #26276 ), #4433, .F. ) ;
#134908=CARTESIAN_POINT ( 'NONE',  ( 0.000000000000000000, 0.000000000000000000, 5.000000000000000000 ) ) ;
#134909=ORIENTED_EDGE ( 'NONE', *, *, #61510, .T. ) ;
#134910=VERTEX_POINT ( 'NONE', #58960 ) ;
#134912=VERTEX_POINT ( 'NONE', #5195 ) ;
#134913=AXIS2_PLACEMENT_3D ( 'NONE', #88722, #130806, #65563 ) ;
#134914=AXIS2_PLACEMENT_3D ( 'NONE', #130863, #29363, #73606 ) ;
#134915=CARTESIAN_POINT ( 'NONE',  ( 12.32816939922344623, -15.74070752338411694, 4.000000000000000000 ) ) ;
#134916=VECTOR ( 'NONE', #130460, 1000.000000000000000 ) ;
#134917=PLANE ( 'NONE',  #72995 ) ;
#134920=ORIENTED_EDGE ( 'NONE', *, *, #118263, .F. ) ;
#134921=DIRECTION ( 'NONE',  ( 0.7071067811865486830, -0.7071067811865464625, -0.000000000000000000 ) ) ;
#134922=AXIS2_PLACEMENT_3D ( 'NONE', #109696, #11060, #9646 ) ;
#134924=DIRECTION ( 'NONE',  ( 1.000000000000000000, 0.000000000000000000, 0.000000000000000000 ) ) ;
#134926=FACE_BOUND ( 'NONE', #54069, .T. ) ;
#134927=ORIENTED_EDGE ( 'NONE', *, *, #106994, .F. ) ;
#134928=CARTESIAN_POINT ( 'NONE',  ( -1.499999999999994449, 16.18958161055402911, -11.56426086740811776 ) ) ;
#134929=LINE ( 'NONE', #2189, #83166 ) ;
#134930=PLANE ( 'NONE',  #95448 ) ;
#134931=EDGE_CURVE ( 'NONE', #8819, #5949, #70538, .T. ) ;
#134932=VERTEX_POINT ( 'NONE', #93675 ) ;
#134933=CARTESIAN_POINT ( 'NONE',  ( 27.18398860626900060, 28.73617430169806042, 5.000000000000000000 ) ) ;
#134935=ORIENTED_EDGE ( 'NONE', *, *, #80351, .T. ) ;
#134936=EDGE_LOOP ( 'NONE', ( #45017, #33917, #135816, #118775 ) ) ;
#134937=EDGE_CURVE ( 'NONE', #109252, #133102, #123472, .T. ) ;
#134939=VERTEX_POINT ( 'NONE', #35757 ) ;
#134940=VECTOR ( 'NONE', #31563, 1000.000000000000000 ) ;
#134941=DIRECTION ( 'NONE',  ( 0.7071067811865487940, 0.7071067811865463515, -0.000000000000000000 ) ) ;
#134942=EDGE_CURVE ( 'NONE', #71967, #12285, #136440, .T. ) ;
#134944=ORIENTED_EDGE ( 'NONE', *, *, #5213, .F. ) ;
#134945=CARTESIAN_POINT ( 'NONE',  ( 16.78501580275800720, -3.740707523384238176, 15.76143240460127792 ) ) ;
#134946=VECTOR ( 'NONE', #61659, 1000.000000000000000 ) ;
#134947=ADVANCED_FACE ( 'NONE', ( #112559 ), #25539, .F. ) ;
#134948=CARTESIAN_POINT ( 'NONE',  ( -21.48921356237309155, -27.52281430457070499, 5.000000000000000000 ) ) ;
#134950=VECTOR ( 'NONE', #139452, 1000.000000000000000 ) ;
#134952=VERTEX_POINT ( 'NONE', #57491 ) ;
#134953=EDGE_LOOP ( 'NONE', ( #109647, #6197, #74826, #4570 ) ) ;
#134954=ORIENTED_EDGE ( 'NONE', *, *, #14273, .T. ) ;
#134958=ORIENTED_EDGE ( 'NONE', *, *, #138484, .F. ) ;
#134960=LINE ( 'NONE', #35651, #76797 ) ;
#134961=ADVANCED_FACE ( 'NONE', ( #35027 ), #69812, .F. ) ;
#134962=CARTESIAN_POINT ( 'NONE',  ( -34.49999999999975131, -16.91253812416058366, 4.000000000000000000 ) ) ;
#134964=CARTESIAN_POINT ( 'NONE',  ( 8.292893218813404133, -18.74070752338409562, 5.000000000000000000 ) ) ;
#134967=CARTESIAN_POINT ( 'NONE',  ( 2.816011393730999401, 28.73617430169785436, 5.000000000000000000 ) ) ;
#134968=VERTEX_POINT ( 'NONE', #81394 ) ;
#134970=CARTESIAN_POINT ( 'NONE',  ( -9.792893218813384593, -14.24070752338413470, 5.000000000000000000 ) ) ;
#134971=CARTESIAN_POINT ( 'NONE',  ( 34.49999999999975842, 16.08746187583908949, 4.000000000000000000 ) ) ;
#134972=CARTESIAN_POINT ( 'NONE',  ( -34.47516574401892342, -7.509482387884301779, 4.998110765256835286 ) ) ;
#134973=CIRCLE ( 'NONE', #23810, 5.968999999999998529 ) ;
#134974=ORIENTED_EDGE ( 'NONE', *, *, #16201, .T. ) ;
#134975=LINE ( 'NONE', #11697, #56536 ) ;
#134977=ORIENTED_EDGE ( 'NONE', *, *, #92794, .F. ) ;
#134978=LINE ( 'NONE', #33523, #57837 ) ;
#134979=VECTOR ( 'NONE', #112714, 1000.000000000000000 ) ;
#134980=ORIENTED_EDGE ( 'NONE', *, *, #30240, .T. ) ;
#134982=CARTESIAN_POINT ( 'NONE',  ( 11.99999999999992362, 17.58746187583906107, 4.000000000000000000 ) ) ;
#134983=CARTESIAN_POINT ( 'NONE',  ( 6.850051285410198254, -8.240707523384193323, 17.25253755692240532 ) ) ;
#134985=VERTEX_POINT ( 'NONE', #103794 ) ;
#134986=DIRECTION ( 'NONE',  ( -0.000000000000000000, 0.000000000000000000, 1.000000000000000000 ) ) ;
#134987=DIRECTION ( 'NONE',  ( -0.7071067811865486830, 0.7071067811865464625, 0.000000000000000000 ) ) ;
#134988=DIRECTION ( 'NONE',  ( -1.000000000000000000, 0.000000000000000000, 0.000000000000000000 ) ) ;
#134989=ORIENTED_EDGE ( 'NONE', *, *, #99707, .F. ) ;
#134990=VECTOR ( 'NONE', #78009, 1000.000000000000000 ) ;
#134991=CARTESIAN_POINT ( 'NONE',  ( 22.49999999999984368, -1.695981523266237634, 4.571483868317931964 ) ) ;
#134992=ORIENTED_EDGE ( 'NONE', *, *, #47976, .T. ) ;
#134993=CARTESIAN_POINT ( 'NONE',  ( -39.18398860626899705, 28.73617430169814568, 5.000000000000000000 ) ) ;
#134994=FACE_OUTER_BOUND ( 'NONE', #48096, .T. ) ;
#134996=EDGE_CURVE ( 'NONE', #14052, #98566, #135065, .T. ) ;
#134997=ORIENTED_EDGE ( 'NONE', *, *, #2826, .T. ) ;
#134998=VECTOR ( 'NONE', #1267, 1000.000000000000000 ) ;
#134999=DIRECTION ( 'NONE',  ( -0.7071067811865486830, -0.7071067811865464625, 0.000000000000000000 ) ) ;
#135000=CARTESIAN_POINT ( 'NONE',  ( -7.499999999999951150, -12.66682484999667224, -0.6294897503864105293 ) ) ;
#135002=EDGE_CURVE ( 'NONE', #24379, #54976, #124147, .T. ) ;
#135003=EDGE_CURVE ( 'NONE', #18734, #23623, #125601, .T. ) ;
#135005=EDGE_CURVE ( 'NONE', #102417, #35044, #47366, .T. ) ;
#135006=EDGE_LOOP ( 'NONE', ( #68352, #58946, #55095, #94876 ) ) ;
#135007=LINE ( 'NONE', #24775, #72063 ) ;
#135008=EDGE_CURVE ( 'NONE', #36381, #66501, #46647, .T. ) ;
#135009=LINE ( 'NONE', #122657, #76824 ) ;
#135010=DIRECTION ( 'NONE',  ( 0.7071067811865487940, 0.7071067811865463515, 0.000000000000000000 ) ) ;
#135011=VECTOR ( 'NONE', #37634, 1000.000000000000000 ) ;
#135013=DIRECTION ( 'NONE',  ( -0.000000000000000000, 0.000000000000000000, 1.000000000000000000 ) ) ;
#135014=EDGE_CURVE ( 'NONE', #80414, #136986, #113253, .T. ) ;
#135017=ORIENTED_EDGE ( 'NONE', *, *, #72818, .F. ) ;
#135018=AXIS2_PLACEMENT_3D ( 'NONE', #125656, #94422, #137957 ) ;
#135019=ORIENTED_EDGE ( 'NONE', *, *, #74489, .F. ) ;
#135020=ORIENTED_EDGE ( 'NONE', *, *, #82655, .F. ) ;
#135022=EDGE_CURVE ( 'NONE', #2765, #114790, #80665, .T. ) ;
#135024=ORIENTED_EDGE ( 'NONE', *, *, #4528, .T. ) ;
#135025=ORIENTED_EDGE ( 'NONE', *, *, #69185, .F. ) ;
#135026=VECTOR ( 'NONE', #50252, 1000.000000000000000 ) ;
#135027=VECTOR ( 'NONE', #117855, 1000.000000000000000 ) ;
#135031=VERTEX_POINT ( 'NONE', #41414 ) ;
#135032=DIRECTION ( 'NONE',  ( 0.7071067811865486830, -0.7071067811865464625, -0.000000000000000000 ) ) ;
#135034=EDGE_CURVE ( 'NONE', #28318, #8822, #85620, .T. ) ;
#135035=CARTESIAN_POINT ( 'NONE',  ( -19.49999999999986500, 12.05218569542904383, 5.000000000000000000 ) ) ;
#135036=DIRECTION ( 'NONE',  ( -0.7071067811865487940, 0.7071067811865463515, 0.000000000000000000 ) ) ;
#135038=ORIENTED_EDGE ( 'NONE', *, *, #39142, .T. ) ;
#135039=FACE_OUTER_BOUND ( 'NONE', #20583, .T. ) ;
#135040=CARTESIAN_POINT ( 'NONE',  ( -30.79333936457826226, 21.75929247661549581, 4.998822639870701856 ) ) ;
#135041=LINE ( 'NONE', #90054, #49560 ) ;
#135042=DIRECTION ( 'NONE',  ( -0.3543493200069162685, -0.000000000000000000, -0.9351131265310288487 ) ) ;
#135043=LINE ( 'NONE', #104507, #75315 ) ;
#135044=EDGE_CURVE ( 'NONE', #121175, #74390, #30561, .T. ) ;
#135045=FACE_OUTER_BOUND ( 'NONE', #70982, .T. ) ;
#135046=LINE ( 'NONE', #92924, #20320 ) ;
#135050=LINE ( 'NONE', #122693, #117817 ) ;
#135051=ORIENTED_EDGE ( 'NONE', *, *, #21934, .F. ) ;
#135052=VERTEX_POINT ( 'NONE', #106653 ) ;
#135054=VERTEX_POINT ( 'NONE', #50878 ) ;
#135055=LINE ( 'NONE', #102415, #23045 ) ;
#135056=LINE ( 'NONE', #14670, #67049 ) ;
#135059=VECTOR ( 'NONE', #123720, 999.9999999999998863 ) ;
#135060=CARTESIAN_POINT ( 'NONE',  ( 32.99999999999977973, 7.552185695429098899, 5.000000000000000000 ) ) ;
#135062=AXIS2_PLACEMENT_3D ( 'NONE', #6696, #127086, #72775 ) ;
#135063=ORIENTED_EDGE ( 'NONE', *, *, #143232, .T. ) ;
#135064=EDGE_CURVE ( 'NONE', #13774, #62936, #7342, .T. ) ;
#135065=LINE ( 'NONE', #48746, #121975 ) ;
#135066=ORIENTED_EDGE ( 'NONE', *, *, #72475, .T. ) ;
#135068=DIRECTION ( 'NONE',  ( 0.7071067811865487940, 0.7071067811865463515, 0.000000000000000000 ) ) ;
#135069=DIRECTION ( 'NONE',  ( -0.7071067811865486830, -0.7071067811865464625, 0.000000000000000000 ) ) ;
#135070=EDGE_CURVE ( 'NONE', #40303, #16626, #29817, .T. ) ;
#135071=AXIS2_PLACEMENT_3D ( 'NONE', #138163, #131569, #55442 ) ;
#135072=DIRECTION ( 'NONE',  ( -0.6830127018922180770, 0.6830127018922202975, -0.2588190451025213501 ) ) ;
#135073=ORIENTED_EDGE ( 'NONE', *, *, #77838, .F. ) ;
#135074=CARTESIAN_POINT ( 'NONE',  ( -8.292893218813391698, 20.25929247661551003, 5.000000000000000000 ) ) ;
#135075=ORIENTED_EDGE ( 'NONE', *, *, #119317, .F. ) ;
#135077=DIRECTION ( 'NONE',  ( -0.3543493200069162685, -0.000000000000000000, -0.9351131265310288487 ) ) ;
#135078=LINE ( 'NONE', #35770, #91756 ) ;
#135079=DIRECTION ( 'NONE',  ( -0.7071067811865486830, -0.7071067811865464625, 0.000000000000000000 ) ) ;
#135080=LINE ( 'NONE', #34303, #115598 ) ;
#135081=EDGE_CURVE ( 'NONE', #35471, #50028, #84927, .T. ) ;
#135082=AXIS2_PLACEMENT_3D ( 'NONE', #114885, #126497, #48240 ) ;
#135084=LINE ( 'NONE', #55358, #29139 ) ;
#135090=ORIENTED_EDGE ( 'NONE', *, *, #47798, .F. ) ;
#135091=ORIENTED_EDGE ( 'NONE', *, *, #133433, .T. ) ;
#135092=AXIS2_PLACEMENT_3D ( 'NONE', #1019, #124951, #110489 ) ;
#135093=CARTESIAN_POINT ( 'NONE',  ( 4.171830600776440079, 12.75929247661559351, 4.000000000000000000 ) ) ;
#135094=ORIENTED_EDGE ( 'NONE', *, *, #97993, .F. ) ;
#135101=ADVANCED_FACE ( 'NONE', ( #107387 ), #51605, .F. ) ;
#135102=FACE_BOUND ( 'NONE', #87512, .T. ) ;
#135103=CARTESIAN_POINT ( 'NONE',  ( -14.09068777029287567, 6.496774105546209377, 4.000000000000000000 ) ) ;
#135104=EDGE_CURVE ( 'NONE', #139894, #79492, #82808, .T. ) ;
#135108=CARTESIAN_POINT ( 'NONE',  ( -19.49999999999987210, -2.777013188829482893, 4.549262955118030582 ) ) ;
#135109=ORIENTED_EDGE ( 'NONE', *, *, #12421, .F. ) ;
#135112=ORIENTED_EDGE ( 'NONE', *, *, #136647, .T. ) ;
#135113=ORIENTED_EDGE ( 'NONE', *, *, #127966, .T. ) ;
#135115=ORIENTED_EDGE ( 'NONE', *, *, #96828, .T. ) ;
#135116=DIRECTION ( 'NONE',  ( 0.7071067811865487940, 0.7071067811865463515, 0.000000000000000000 ) ) ;
#135117=ORIENTED_EDGE ( 'NONE', *, *, #25225, .T. ) ;
#135118=LINE ( 'NONE', #112615, #65331 ) ;
#135119=VECTOR ( 'NONE', #142248, 1000.000000000000000 ) ;
#135121=EDGE_CURVE ( 'NONE', #54378, #127190, #118244, .T. ) ;
#135122=PLANE ( 'NONE',  #119644 ) ;
#135123=CARTESIAN_POINT ( 'NONE',  ( 0.000000000000000000, 0.000000000000000000, 5.000000000000000000 ) ) ;
#135124=DIRECTION ( 'NONE',  ( 0.6830127018922180770, -0.6830127018922204085, -0.2588190451025213501 ) ) ;
#135125=CARTESIAN_POINT ( 'NONE',  ( 14.99999999999989697, -9.412538124160656494, 4.000000000000000000 ) ) ;
#135126=CARTESIAN_POINT ( 'NONE',  ( 0.000000000000000000, 0.000000000000000000, 5.000000000000000000 ) ) ;
#135128=VECTOR ( 'NONE', #15200, 1000.000000000000000 ) ;
#135129=ORIENTED_EDGE ( 'NONE', *, *, #77584, .F. ) ;
#135130=CARTESIAN_POINT ( 'NONE',  ( 24.99581563014004715, 3.703558271726553830, 4.317415941188023076 ) ) ;
#135132=EDGE_LOOP ( 'NONE', ( #88796, #45107, #2985, #107665 ) ) ;
#135133=ORIENTED_EDGE ( 'NONE', *, *, #139445, .F. ) ;
#135134=ORIENTED_EDGE ( 'NONE', *, *, #58039, .T. ) ;
#135137=ORIENTED_EDGE ( 'NONE', *, *, #109008, .T. ) ;
#135139=AXIS2_PLACEMENT_3D ( 'NONE', #9516, #44350, #125274 ) ;
#135140=CARTESIAN_POINT ( 'NONE',  ( -8.292893218813397027, -18.74070752338409562, 5.000000000000000000 ) ) ;
#135141=VECTOR ( 'NONE', #139101, 1000.000000000000227 ) ;
#135145=DIRECTION ( 'NONE',  ( -0.6830127018922181881, 0.6830127018922202975, -0.2588190451025214056 ) ) ;
#135146=DIRECTION ( 'NONE',  ( -0.6830127018922181881, 0.6830127018922202975, -0.2588190451025214056 ) ) ;
#135147=CARTESIAN_POINT ( 'NONE',  ( -39.33010218547241266, 17.25929247661553845, 19.83885114516080606 ) ) ;
#135148=LINE ( 'NONE', #45287, #77314 ) ;
#135149=EDGE_LOOP ( 'NONE', ( #90321, #120492, #30588, #34561 ) ) ;
#135151=CARTESIAN_POINT ( 'NONE',  ( 34.49999999999975842, -16.53574439159934073, 4.994342998332164107 ) ) ;
#135152=LINE ( 'NONE', #134420, #21365 ) ;
#135153=AXIS2_PLACEMENT_3D ( 'NONE', #9564, #53837, #131381 ) ;
#135154=PLANE ( 'NONE',  #137407 ) ;
#135155=ORIENTED_EDGE ( 'NONE', *, *, #142204, .F. ) ;
#135157=DIRECTION ( 'NONE',  ( -0.7071067811865486830, -0.7071067811865464625, 0.000000000000000000 ) ) ;
#135159=CARTESIAN_POINT ( 'NONE',  ( -25.49999999999981526, 1.087461875839237591, 4.000000000000000000 ) ) ;
#135161=DIRECTION ( 'NONE',  ( -0.7071067811865486830, -0.7071067811865464625, 0.000000000000000000 ) ) ;
#135162=CARTESIAN_POINT ( 'NONE',  ( -12.70710678118645198, -6.740707523384211086, 5.000000000000000000 ) ) ;
#135163=PLANE ( 'NONE',  #2958 ) ;
#135164=( BOUNDED_CURVE ( )  B_SPLINE_CURVE ( 3, ( #64163, #131557, #8994, #20627 ),
 .UNSPECIFIED., .F., .T. ) 
 B_SPLINE_CURVE_WITH_KNOTS ( ( 4, 4 ),
 ( 2.001653308786175867, 3.503810798801451742 ),
 .UNSPECIFIED. ) 
 CURVE ( )  GEOMETRIC_REPRESENTATION_ITEM ( )  RATIONAL_B_SPLINE_CURVE ( ( 1.000000000000000000, 0.8206354192515253887, 0.8206354192515253887, 1.000000000000000000 ) ) 
 REPRESENTATION_ITEM ( '' )  );
#135166=CARTESIAN_POINT ( 'NONE',  ( -5.999999999999963585, -13.39766691384884290, -10.96608748226464414 ) ) ;
#135168=VERTEX_POINT ( 'NONE', #27677 ) ;
#135169=ORIENTED_EDGE ( 'NONE', *, *, #28115, .F. ) ;
#135171=CARTESIAN_POINT ( 'NONE',  ( -19.17183060077633883, 18.75929247661552068, 4.000000000000000000 ) ) ;
#135173=DIRECTION ( 'NONE',  ( 0.000000000000000000, 0.000000000000000000, -1.000000000000000000 ) ) ;
#135174=CARTESIAN_POINT ( 'NONE',  ( 0.000000000000000000, -21.72500000000000142, 4.500000000000000888 ) ) ;
#135175=ADVANCED_FACE ( 'NONE', ( #63904 ), #71947, .F. ) ;
#135176=VECTOR ( 'NONE', #4896, 1000.000000000000000 ) ;
#135178=PLANE ( 'NONE',  #22800 ) ;
#135179=ADVANCED_FACE ( 'NONE', ( #96476 ), #52992, .F. ) ;
#135180=EDGE_CURVE ( 'NONE', #3063, #23219, #74055, .T. ) ;
#135181=ORIENTED_EDGE ( 'NONE', *, *, #61257, .F. ) ;
#135185=AXIS2_PLACEMENT_3D ( 'NONE', #17129, #60682, #104102 ) ;
#135186=DIRECTION ( 'NONE',  ( 0.7071067811865487940, 0.7071067811865463515, -0.000000000000000000 ) ) ;
#135187=EDGE_CURVE ( 'NONE', #40291, #133314, #140720, .T. ) ;
#135189=LINE ( 'NONE', #24256, #139081 ) ;
#135190=CARTESIAN_POINT ( 'NONE',  ( 22.17183060077632462, 18.75929247661553134, 4.000000000000000000 ) ) ;
#135191=CARTESIAN_POINT ( 'NONE',  ( 5.999999999999963585, 2.342191155542457714, -5.001666872980099043 ) ) ;
#135193=EDGE_CURVE ( 'NONE', #13287, #10331, #39297, .T. ) ;
#135194=VERTEX_POINT ( 'NONE', #83524 ) ;
#135195=VECTOR ( 'NONE', #100367, 999.9999999999998863 ) ;
#135198=CARTESIAN_POINT ( 'NONE',  ( -9.330102185472595622, 17.25929247661553845, 19.83885114516073500 ) ) ;
#135199=EDGE_CURVE ( 'NONE', #107544, #123094, #8054, .T. ) ;
#135200=CARTESIAN_POINT ( 'NONE',  ( -66.48921356237309510, -27.52281430457101763, 5.000000000000000000 ) ) ;
#135201=EDGE_CURVE ( 'NONE', #110885, #53800, #135419, .T. ) ;
#135202=PLANE ( 'NONE',  #76537 ) ;
#135203=CARTESIAN_POINT ( 'NONE',  ( 2.292893218813441880, 8.259292476615639700, 5.000000000000000000 ) ) ;
#135204=ORIENTED_EDGE ( 'NONE', *, *, #81642, .F. ) ;
#135205=ORIENTED_EDGE ( 'NONE', *, *, #64932, .F. ) ;
#135206=CARTESIAN_POINT ( 'NONE',  ( 1.828169399223521507, 18.75929247661552779, 4.000000000000000000 ) ) ;
#135207=CARTESIAN_POINT ( 'NONE',  ( -33.48921356237309510, -27.52281430457078670, 5.000000000000000000 ) ) ;
#135208=CARTESIAN_POINT ( 'NONE',  ( -22.49999999999984013, -19.91253812416055879, 4.000000000000000000 ) ) ;
#135209=EDGE_CURVE ( 'NONE', #15478, #135598, #12171, .T. ) ;
#135210=PLANE ( 'NONE',  #101260 ) ;
#135213=AXIS2_PLACEMENT_3D ( 'NONE', #135825, #48113, #37220 ) ;
#135215=ORIENTED_EDGE ( 'NONE', *, *, #21229, .T. ) ;
#135217=CARTESIAN_POINT ( 'NONE',  ( 36.48921356237310221, -27.52281430457080802, 5.000000000000000000 ) ) ;
#135218=DIRECTION ( 'NONE',  ( 0.6830127018922181881, 0.6830127018922202975, -0.2588190451025214056 ) ) ;
#135219=CARTESIAN_POINT ( 'NONE',  ( -11.99999999999991118, 7.552185695429091794, 5.000000000000000000 ) ) ;
#135220=ORIENTED_EDGE ( 'NONE', *, *, #73162, .F. ) ;
#135221=AXIS2_PLACEMENT_3D ( 'NONE', #106532, #107954, #41297 ) ;
#135222=LINE ( 'NONE', #92370, #21268 ) ;
#135223=CARTESIAN_POINT ( 'NONE',  ( -8.999999999999936051, -6.033600742197680056, 5.000000000000000000 ) ) ;
#135226=CARTESIAN_POINT ( 'NONE',  ( -29.99999999999977618, 20.58746187583903264, 4.000000000000000000 ) ) ;
#135228=EDGE_LOOP ( 'NONE', ( #130269, #49901, #39383, #101897 ) ) ;
#135229=DIRECTION ( 'NONE',  ( -0.000000000000000000, -0.3543493200069152693, 0.9351131265310292928 ) ) ;
#135231=CARTESIAN_POINT ( 'NONE',  ( -13.09320915088844650, 2.775078171252264081, 4.657771095945246742 ) ) ;
#135232=DIRECTION ( 'NONE',  ( -0.7071067811865487940, 0.7071067811865463515, 0.000000000000000000 ) ) ;
#135234=EDGE_LOOP ( 'NONE', ( #4715, #19113, #5843 ) ) ;
#135238=VECTOR ( 'NONE', #121516, 1000.000000000000000 ) ;
#135239=CARTESIAN_POINT ( 'NONE',  ( 60.48921356237309510, -27.52281430457097500, 5.000000000000000000 ) ) ;
#135240=ORIENTED_EDGE ( 'NONE', *, *, #70023, .F. ) ;
#135241=ORIENTED_EDGE ( 'NONE', *, *, #50413, .F. ) ;
#135244=ORIENTED_EDGE ( 'NONE', *, *, #18314, .F. ) ;
#135245=CARTESIAN_POINT ( 'NONE',  ( -10.49999999999991296, -6.839392718269134974, -8.480912228396059405 ) ) ;
#135246=DIRECTION ( 'NONE',  ( -0.7071067811865486830, -0.7071067811865464625, 0.000000000000000000 ) ) ;
#135247=ADVANCED_FACE ( 'NONE', ( #112920 ), #45565, .F. ) ;
#135248=DIRECTION ( 'NONE',  ( -0.000000000000000000, 0.000000000000000000, 1.000000000000000000 ) ) ;
#135251=ORIENTED_EDGE ( 'NONE', *, *, #61199, .T. ) ;
#135252=CARTESIAN_POINT ( 'NONE',  ( -10.49999999999992895, 11.52377502935401843, -1.522421517564061411 ) ) ;
#135256=EDGE_CURVE ( 'NONE', #88862, #38475, #113625, .T. ) ;
#135257=DIRECTION ( 'NONE',  ( 0.6830127018922181881, 0.6830127018922202975, -0.2588190451025214056 ) ) ;
#135260=CARTESIAN_POINT ( 'NONE',  ( 17.99451991528748351, 28.92564299267950645, 4.000000000000000000 ) ) ;
#135261=CARTESIAN_POINT ( 'NONE',  ( 60.18398860626900415, 28.73617430169829490, 5.000000000000000000 ) ) ;
#135262=ORIENTED_EDGE ( 'NONE', *, *, #92794, .T. ) ;
#135263=VECTOR ( 'NONE', #124093, 1000.000000000000227 ) ;
#135264=VECTOR ( 'NONE', #18289, 1000.000000000000000 ) ;
#135265=ADVANCED_FACE ( 'NONE', ( #102050 ), #134705, .F. ) ;
#135266=FACE_BOUND ( 'NONE', #143305, .T. ) ;
#135267=DIRECTION ( 'NONE',  ( 0.7071067811865486830, -0.7071067811865464625, -0.000000000000000000 ) ) ;
#135268=DIRECTION ( 'NONE',  ( 0.7071067811865487940, 0.7071067811865463515, 0.000000000000000000 ) ) ;
#135269=FACE_OUTER_BOUND ( 'NONE', #44560, .T. ) ;
#135270=CARTESIAN_POINT ( 'NONE',  ( -18.70710678118640402, -6.740707523384209310, 5.000000000000000000 ) ) ;
#135271=AXIS2_PLACEMENT_3D ( 'NONE', #88395, #98530, #121691 ) ;
#135272=CARTESIAN_POINT ( 'NONE',  ( -0.2997448713915885632, -27.71228299555206220, 4.000000000000000000 ) ) ;
#135274=ORIENTED_EDGE ( 'NONE', *, *, #68377, .F. ) ;
#135275=VECTOR ( 'NONE', #93040, 1000.000000000000000 ) ;
#135276=ORIENTED_EDGE ( 'NONE', *, *, #36590, .F. ) ;
#135278=VERTEX_POINT ( 'NONE', #124515 ) ;
#135279=LINE ( 'NONE', #36636, #139179 ) ;
#135280=ORIENTED_EDGE ( 'NONE', *, *, #63338, .T. ) ;
#135282=LINE ( 'NONE', #35966, #126501 ) ;
#135283=LINE ( 'NONE', #80887, #40183 ) ;
#135284=ORIENTED_EDGE ( 'NONE', *, *, #28267, .T. ) ;
#135285=CARTESIAN_POINT ( 'NONE',  ( 18.18398860626898994, 28.73617430169800002, 5.000000000000000000 ) ) ;
#135286=EDGE_CURVE ( 'NONE', #139679, #37520, #80326, .T. ) ;
#135287=LINE ( 'NONE', #35970, #3735 ) ;
#135289=LINE ( 'NONE', #103317, #89725 ) ;
#135290=CARTESIAN_POINT ( 'NONE',  ( -18.64318742751726887, -20.24070752338407075, 21.22881796311208191 ) ) ;
#135293=ORIENTED_EDGE ( 'NONE', *, *, #85819, .F. ) ;
#135295=CARTESIAN_POINT ( 'NONE',  ( -30.70701326429283640, -21.74070752338405654, 4.999753212805224223 ) ) ;
#135297=EDGE_CURVE ( 'NONE', #25651, #71266, #23022, .T. ) ;
#135303=ORIENTED_EDGE ( 'NONE', *, *, #138071, .F. ) ;
#135306=DIRECTION ( 'NONE',  ( -0.3543493200069162685, -0.000000000000000000, -0.9351131265310288487 ) ) ;
#135307=ORIENTED_EDGE ( 'NONE', *, *, #86002, .T. ) ;
#135308=DIRECTION ( 'NONE',  ( 0.000000000000000000, -0.3543493200069153248, -0.9351131265310291818 ) ) ;
#135309=EDGE_LOOP ( 'NONE', ( #16303, #77824, #62593, #39616 ) ) ;
#135311=DIRECTION ( 'NONE',  ( -0.000000000000000000, 0.000000000000000000, 1.000000000000000000 ) ) ;
#135312=ORIENTED_EDGE ( 'NONE', *, *, #59279, .T. ) ;
#135313=ADVANCED_FACE ( 'NONE', ( #90463 ), #101330, .F. ) ;
#135314=VECTOR ( 'NONE', #58102, 1000.000000000000227 ) ;
#135316=DIRECTION ( 'NONE',  ( -0.7071067811865486830, -0.7071067811865464625, 0.000000000000000000 ) ) ;
#135318=EDGE_LOOP ( 'NONE', ( #16043, #123652, #48562, #134898 ) ) ;
#135319=DIRECTION ( 'NONE',  ( -0.7071067811865486830, -0.7071067811865464625, 0.000000000000000000 ) ) ;
#135320=VERTEX_POINT ( 'NONE', #133273 ) ;
#135321=VERTEX_POINT ( 'NONE', #35403 ) ;
#135322=VERTEX_POINT ( 'NONE', #13580 ) ;
#135323=CARTESIAN_POINT ( 'NONE',  ( 16.49999999999989342, -14.94781430457067550, 5.000000000000000000 ) ) ;
#135324=FACE_OUTER_BOUND ( 'NONE', #22256, .T. ) ;
#135325=DIRECTION ( 'NONE',  ( -0.3543493200069162685, -0.000000000000000000, -0.9351131265310288487 ) ) ;
#135326=DIRECTION ( 'NONE',  ( -0.7071067811865486830, 0.7071067811865464625, 0.000000000000000000 ) ) ;
#135327=DIRECTION ( 'NONE',  ( -0.7071067811865487940, 0.7071067811865463515, 0.000000000000000000 ) ) ;
#135328=VERTEX_POINT ( 'NONE', #66578 ) ;
#135330=EDGE_CURVE ( 'NONE', #139613, #40545, #89739, .T. ) ;
#135334=ADVANCED_FACE ( 'NONE', ( #86373 ), #112224, .F. ) ;
#135335=DIRECTION ( 'NONE',  ( 0.7071067811865487940, 0.7071067811865463515, 0.000000000000000000 ) ) ;
#135336=LINE ( 'NONE', #113537, #86036 ) ;
#135337=ORIENTED_EDGE ( 'NONE', *, *, #80719, .F. ) ;
#135338=EDGE_CURVE ( 'NONE', #44187, #141351, #123102, .T. ) ;
#135339=VECTOR ( 'NONE', #133067, 999.9999999999998863 ) ;
#135341=ORIENTED_EDGE ( 'NONE', *, *, #108355, .T. ) ;
#135342=CARTESIAN_POINT ( 'NONE',  ( 2.994519915287485734, 28.92564299267940342, 4.000000000000000000 ) ) ;
#135343=CYLINDRICAL_SURFACE ( 'NONE', #9315, 0.5000000000000004441 ) ;
#135344=CARTESIAN_POINT ( 'NONE',  ( 17.99999999999987566, -9.412538124160654718, 4.000000000000000000 ) ) ;
#135345=PLANE ( 'NONE',  #11203 ) ;
#135346=ADVANCED_FACE ( 'NONE', ( #11430 ), #12876, .T. ) ;
#135349=CARTESIAN_POINT ( 'NONE',  ( 19.17183060077633883, -8.240707523384196875, 4.000000000000000000 ) ) ;
#135350=AXIS2_PLACEMENT_3D ( 'NONE', #59229, #92504, #91126 ) ;
#135351=LINE ( 'NONE', #123027, #91194 ) ;
#135352=DIRECTION ( 'NONE',  ( -0.000000000000000000, 0.3543493200069153248, 0.9351131265310292928 ) ) ;
#135354=DIRECTION ( 'NONE',  ( 0.6830127018922181881, 0.6830127018922202975, -0.2588190451025214056 ) ) ;
#135355=CARTESIAN_POINT ( 'NONE',  ( -11.99999999999991118, 18.08204922493371924, 0.9627537363045149954 ) ) ;
#135356=VERTEX_POINT ( 'NONE', #99903 ) ;
#135358=ORIENTED_EDGE ( 'NONE', *, *, #30466, .T. ) ;
#135359=CARTESIAN_POINT ( 'NONE',  ( -13.17183060077637791, 15.75929247661555443, 4.000000000000000000 ) ) ;
#135360=CARTESIAN_POINT ( 'NONE',  ( 2.206660635421510808, 21.75929247661549937, 4.998822639870701856 ) ) ;
#135361=EDGE_LOOP ( 'NONE', ( #113778, #117567, #8657, #106131 ) ) ;
#135362=EDGE_CURVE ( 'NONE', #63259, #137446, #4818, .T. ) ;
#135363=EDGE_CURVE ( 'NONE', #136197, #816, #5566, .T. ) ;
#135365=CARTESIAN_POINT ( 'NONE',  ( 26.20666063542134339, 21.75929247661549581, 4.998822639870700968 ) ) ;
#135366=ORIENTED_EDGE ( 'NONE', *, *, #106503, .F. ) ;
#135367=CARTESIAN_POINT ( 'NONE',  ( 11.70025512860841133, -27.71228299555198049, 4.000000000000000000 ) ) ;
#135368=ORIENTED_EDGE ( 'NONE', *, *, #67953, .F. ) ;
#135369=LINE ( 'NONE', #114970, #141631 ) ;
#135370=EDGE_LOOP ( 'NONE', ( #11482, #100361, #52949, #117456 ) ) ;
#135372=PLANE ( 'NONE',  #22094 ) ;
#135375=PLANE ( 'NONE',  #115720 ) ;
#135376=AXIS2_PLACEMENT_3D ( 'NONE', #120287, #86988, #100018 ) ;
#135377=CARTESIAN_POINT ( 'NONE',  ( -5.994519915287488843, 28.92564299267942118, 4.000000000000000000 ) ) ;
#135378=ORIENTED_EDGE ( 'NONE', *, *, #136210, .F. ) ;
#135379=VECTOR ( 'NONE', #61471, 1000.000000000000000 ) ;
#135381=PLANE ( 'NONE',  #51927 ) ;
#135384=CARTESIAN_POINT ( 'NONE',  ( 0.000000000000000000, 0.000000000000000000, 5.000000000000000000 ) ) ;
#135386=DIRECTION ( 'NONE',  ( -0.3543493200069162685, -0.000000000000000000, -0.9351131265310288487 ) ) ;
#135387=EDGE_LOOP ( 'NONE', ( #104394, #24038, #131438, #106825 ) ) ;
#135389=DIRECTION ( 'NONE',  ( -0.000000000000000000, -0.000000000000000000, 1.000000000000000000 ) ) ;
#135392=CARTESIAN_POINT ( 'NONE',  ( 39.48921356237310221, -27.52281430457082934, 5.000000000000000000 ) ) ;
#135393=CARTESIAN_POINT ( 'NONE',  ( -19.49999999999986500, -6.839392718269142080, -8.480912228396038088 ) ) ;
#135394=EDGE_CURVE ( 'NONE', #125758, #102340, #81028, .T. ) ;
#135396=CARTESIAN_POINT ( 'NONE',  ( -34.17183060077623225, -8.240707523384200428, 4.000000000000000000 ) ) ;
#135397=VERTEX_POINT ( 'NONE', #94708 ) ;
#135399=CARTESIAN_POINT ( 'NONE',  ( 23.99999999999984013, -3.412538124160721331, 4.000000000000000000 ) ) ;
#135400=VERTEX_POINT ( 'NONE', #3420 ) ;
#135401=CARTESIAN_POINT ( 'NONE',  ( -6.005480084712508493, 28.92564299267933947, 4.000000000000000000 ) ) ;
#135403=CARTESIAN_POINT ( 'NONE',  ( -17.29289321881333308, -6.740707523384211086, 5.000000000000000000 ) ) ;
#135404=VERTEX_POINT ( 'NONE', #59983 ) ;
#135405=ADVANCED_FACE ( 'NONE', ( #138249 ), #47713, .F. ) ;
#135406=EDGE_CURVE ( 'NONE', #66395, #56761, #103453, .T. ) ;
#135407=DIRECTION ( 'NONE',  ( -0.3543493200069162685, -0.000000000000000000, -0.9351131265310288487 ) ) ;
#135408=DIRECTION ( 'NONE',  ( 0.6830127018922181881, 0.6830127018922202975, -0.2588190451025214056 ) ) ;
#135409=DIRECTION ( 'NONE',  ( -0.000000000000000000, 0.000000000000000000, 1.000000000000000000 ) ) ;
#135411=ORIENTED_EDGE ( 'NONE', *, *, #95833, .F. ) ;
#135412=EDGE_CURVE ( 'NONE', #19799, #121985, #49837, .T. ) ;
#135413=ORIENTED_EDGE ( 'NONE', *, *, #67377, .F. ) ;
#135414=ORIENTED_EDGE ( 'NONE', *, *, #35186, .F. ) ;
#135416=ORIENTED_EDGE ( 'NONE', *, *, #44867, .T. ) ;
#135417=DIRECTION ( 'NONE',  ( 0.3543493200069162685, -0.000000000000000000, -0.9351131265310288487 ) ) ;
#135418=DIRECTION ( 'NONE',  ( -0.000000000000000000, -0.3543493200069152693, 0.9351131265310292928 ) ) ;
#135419=LINE ( 'NONE', #23781, #119786 ) ;
#135420=LINE ( 'NONE', #35404, #80507 ) ;
#135421=ORIENTED_EDGE ( 'NONE', *, *, #18051, .F. ) ;
#135424=AXIS2_PLACEMENT_3D ( 'NONE', #89108, #45621, #124574 ) ;
#135428=PLANE ( 'NONE',  #132374 ) ;
#135432=CARTESIAN_POINT ( 'NONE',  ( -29.99999999999979039, -9.033600742197645417, 5.000000000000000000 ) ) ;
#135435=FACE_OUTER_BOUND ( 'NONE', #115941, .T. ) ;
#135437=DIRECTION ( 'NONE',  ( -0.000000000000000000, 0.000000000000000000, 1.000000000000000000 ) ) ;
#135439=AXIS2_PLACEMENT_3D ( 'NONE', #96823, #28046, #30914 ) ;
#135440=ORIENTED_EDGE ( 'NONE', *, *, #113757, .F. ) ;
#135444=ORIENTED_EDGE ( 'NONE', *, *, #14051, .F. ) ;
#135445=EDGE_LOOP ( 'NONE', ( #62348, #26512, #25507, #55963 ) ) ;
#135446=CARTESIAN_POINT ( 'NONE',  ( -9.475126127850408864, 14.25929247661557220, 9.797011795316615590 ) ) ;
#135450=DIRECTION ( 'NONE',  ( 0.7071067811865487940, 0.7071067811865463515, 0.000000000000000000 ) ) ;
#135451=DIRECTION ( 'NONE',  ( 1.000000000000000000, 0.000000000000000000, 0.000000000000000000 ) ) ;
#135452=PLANE ( 'NONE',  #67697 ) ;
#135453=ORIENTED_EDGE ( 'NONE', *, *, #76437, .F. ) ;
#135455=VERTEX_POINT ( 'NONE', #61444 ) ;
#135456=ADVANCED_FACE ( 'NONE', ( #116491 ), #128102, .F. ) ;
#135457=DIRECTION ( 'NONE',  ( -0.7071067811865486830, -0.7071067811865464625, -0.000000000000000000 ) ) ;
#135458=VERTEX_POINT ( 'NONE', #71571 ) ;
#135459=ORIENTED_EDGE ( 'NONE', *, *, #89753, .T. ) ;
#135460=LINE ( 'NONE', #60036, #106010 ) ;
#135461=EDGE_CURVE ( 'NONE', #114304, #96071, #4093, .T. ) ;
#135463=VERTEX_POINT ( 'NONE', #25915 ) ;
#135464=LINE ( 'NONE', #43608, #4739 ) ;
#135465=ORIENTED_EDGE ( 'NONE', *, *, #67875, .F. ) ;
#135466=VECTOR ( 'NONE', #16219, 999.9999999999998863 ) ;
#135467=DIRECTION ( 'NONE',  ( -0.7071067811865487940, 0.7071067811865463515, 0.000000000000000000 ) ) ;
#135468=VECTOR ( 'NONE', #72036, 1000.000000000000000 ) ;
#135469=VECTOR ( 'NONE', #8461, 1000.000000000000000 ) ;
#135470=DIRECTION ( 'NONE',  ( -0.7071067811865486830, 0.7071067811865464625, 0.000000000000000000 ) ) ;
#135472=DIRECTION ( 'NONE',  ( 0.6830127018922180770, -0.6830127018922204085, -0.2588190451025213501 ) ) ;
#135473=VECTOR ( 'NONE', #72379, 1000.000000000000227 ) ;
#135474=EDGE_CURVE ( 'NONE', #53161, #100056, #91875, .T. ) ;
#135475=CARTESIAN_POINT ( 'NONE',  ( -1.499999999999987566, -4.796895815301023269, -3.611700055028684631 ) ) ;
#135476=DIRECTION ( 'NONE',  ( -0.3543493200069162685, -0.000000000000000000, -0.9351131265310288487 ) ) ;
#135477=DIRECTION ( 'NONE',  ( -0.6830127018922180770, -0.6830127018922204085, -0.2588190451025213501 ) ) ;
#135478=EDGE_CURVE ( 'NONE', #118358, #89658, #115731, .T. ) ;
#135479=DIRECTION ( 'NONE',  ( -0.3543493200069162685, -0.000000000000000000, -0.9351131265310288487 ) ) ;
#135482=FACE_OUTER_BOUND ( 'NONE', #140300, .T. ) ;
#135483=ORIENTED_EDGE ( 'NONE', *, *, #95825, .T. ) ;
#135484=ORIENTED_EDGE ( 'NONE', *, *, #132915, .F. ) ;
#135485=CARTESIAN_POINT ( 'NONE',  ( 24.18398860626899705, 28.73617430169804265, 5.000000000000000000 ) ) ;
#135486=EDGE_CURVE ( 'NONE', #48518, #91920, #28059, .T. ) ;
#135488=FACE_OUTER_BOUND ( 'NONE', #57253, .T. ) ;
#135489=CARTESIAN_POINT ( 'NONE',  ( -41.99451991528749062, 28.92564299267967343, 4.000000000000000000 ) ) ;
#135490=CARTESIAN_POINT ( 'NONE',  ( 38.99451991528749062, 28.92564299267965211, 4.000000000000000000 ) ) ;
#135491=CARTESIAN_POINT ( 'NONE',  ( 10.49999999999993250, 0.4497235411627560353, -5.599840258123518488 ) ) ;
#135492=ORIENTED_EDGE ( 'NONE', *, *, #128203, .T. ) ;
#135494=VERTEX_POINT ( 'NONE', #28785 ) ;
#135495=CARTESIAN_POINT ( 'NONE',  ( -25.49999999999982236, -16.53360074219757081, 5.000000000000000000 ) ) ;
#135497=ORIENTED_EDGE ( 'NONE', *, *, #135610, .T. ) ;
#135499=CARTESIAN_POINT ( 'NONE',  ( 26.48334561358936412, 22.22500000000000142, 4.500000000000000888 ) ) ;
#135500=ORIENTED_EDGE ( 'NONE', *, *, #116154, .F. ) ;
#135501=EDGE_CURVE ( 'NONE', #3029, #133340, #39671, .T. ) ;
#135502=VERTEX_POINT ( 'NONE', #117178 ) ;
#135503=ORIENTED_EDGE ( 'NONE', *, *, #43411, .T. ) ;
#135504=DIRECTION ( 'NONE',  ( -0.6830127018922181881, 0.6830127018922202975, -0.2588190451025214056 ) ) ;
#135505=LINE ( 'NONE', #122451, #136646 ) ;
#135506=FACE_OUTER_BOUND ( 'NONE', #21782, .T. ) ;
#135507=FACE_OUTER_BOUND ( 'NONE', #113025, .T. ) ;
#135508=ORIENTED_EDGE ( 'NONE', *, *, #140915, .F. ) ;
#135509=CARTESIAN_POINT ( 'NONE',  ( 17.68342038867199051, -6.740707523384219968, 11.88629033278119884 ) ) ;
#135511=EDGE_CURVE ( 'NONE', #54370, #94334, #114349, .T. ) ;
#135512=CARTESIAN_POINT ( 'NONE',  ( -13.11151487241215108, 3.778085383357084659, 4.109577000315249862 ) ) ;
#135513=LINE ( 'NONE', #69556, #92981 ) ;
#135514=DIRECTION ( 'NONE',  ( 0.6830127018922180770, -0.6830127018922204085, -0.2588190451025213501 ) ) ;
#135515=VERTEX_POINT ( 'NONE', #81760 ) ;
#135517=EDGE_CURVE ( 'NONE', #117707, #18279, #26628, .T. ) ;
#135520=ORIENTED_EDGE ( 'NONE', *, *, #92626, .F. ) ;
#135523=EDGE_CURVE ( 'NONE', #117707, #288, #30929, .T. ) ;
#135524=LINE ( 'NONE', #124627, #77127 ) ;
#135525=PLANE ( 'NONE',  #103950 ) ;
#135526=ORIENTED_EDGE ( 'NONE', *, *, #22975, .F. ) ;
#135527=CARTESIAN_POINT ( 'NONE',  ( 3.707106781186523481, 17.25929247661554200, 5.000000000000000000 ) ) ;
#135528=ORIENTED_EDGE ( 'NONE', *, *, #113226, .T. ) ;
#135529=DIRECTION ( 'NONE',  ( 1.000000000000000000, 0.000000000000000000, 0.000000000000000000 ) ) ;
#135530=FACE_OUTER_BOUND ( 'NONE', #11986, .T. ) ;
#135531=VECTOR ( 'NONE', #14840, 1000.000000000000227 ) ;
#135532=LINE ( 'NONE', #36218, #55447 ) ;
#135533=EDGE_CURVE ( 'NONE', #73204, #122401, #12311, .T. ) ;
#135534=CARTESIAN_POINT ( 'NONE',  ( -11.29289321881337571, -3.740707523384243505, 5.000000000000000000 ) ) ;
#135535=VECTOR ( 'NONE', #33786, 1000.000000000000000 ) ;
#135536=PLANE ( 'NONE',  #136895 ) ;
#135537=CARTESIAN_POINT ( 'NONE',  ( -11.51078643762690490, -27.52281430457047406, 5.000000000000000000 ) ) ;
#135538=DIRECTION ( 'NONE',  ( 1.000000000000000000, 0.000000000000000000, 0.000000000000000000 ) ) ;
#135539=CARTESIAN_POINT ( 'NONE',  ( -34.92500000000001137, 22.22500000000000142, 4.500000000000000888 ) ) ;
#135542=CARTESIAN_POINT ( 'NONE',  ( 23.16170612452605226, -6.740707523384209310, 16.75550250614872638 ) ) ;
#135544=DIRECTION ( 'NONE',  ( 0.7071067811865487940, 0.7071067811865463515, -0.000000000000000000 ) ) ;
#135545=FACE_OUTER_BOUND ( 'NONE', #139410, .T. ) ;
#135546=ORIENTED_EDGE ( 'NONE', *, *, #119335, .T. ) ;
#135547=( BOUNDED_CURVE ( )  B_SPLINE_CURVE ( 3, ( #113161, #23288, #67567, #12426 ),
 .UNSPECIFIED., .F., .F. ) 
 B_SPLINE_CURVE_WITH_KNOTS ( ( 4, 4 ),
 ( 2.972453342939735066, 3.211474374380906660 ),
 .UNSPECIFIED. ) 
 CURVE ( )  GEOMETRIC_REPRESENTATION_ITEM ( )  RATIONAL_B_SPLINE_CURVE ( ( 1.000000000000000000, 0.9952447427727517670, 0.9952447427727517670, 1.000000000000000000 ) ) 
 REPRESENTATION_ITEM ( '' )  );
#135548=ORIENTED_EDGE ( 'NONE', *, *, #53151, .F. ) ;
#135550=VERTEX_POINT ( 'NONE', #118619 ) ;
#135551=VECTOR ( 'NONE', #81888, 1000.000000000000227 ) ;
#135552=ORIENTED_EDGE ( 'NONE', *, *, #107002, .T. ) ;
#135553=ORIENTED_EDGE ( 'NONE', *, *, #69080, .T. ) ;
#135555=CARTESIAN_POINT ( 'NONE',  ( -8.700255128608413102, -27.71228299555199825, 4.000000000000000000 ) ) ;
#135557=ORIENTED_EDGE ( 'NONE', *, *, #86931, .T. ) ;
#135558=CARTESIAN_POINT ( 'NONE',  ( 16.60343192894632480, -14.24070752338413293, 19.24067776001729513 ) ) ;
#135559=DIRECTION ( 'NONE',  ( -0.7071067811865487940, 0.7071067811865463515, -0.000000000000000000 ) ) ;
#135560=FACE_OUTER_BOUND ( 'NONE', #68448, .T. ) ;
#135563=FACE_OUTER_BOUND ( 'NONE', #29323, .T. ) ;
#135564=CARTESIAN_POINT ( 'NONE',  ( -27.64318742751720848, -20.24070752338407786, 21.22881796311206770 ) ) ;
#135565=CARTESIAN_POINT ( 'NONE',  ( 34.75611968250419181, 14.81293425470724046, 4.955485411084880276 ) ) ;
#135567=DIRECTION ( 'NONE',  ( 0.000000000000000000, 1.000000000000000000, -0.000000000000000000 ) ) ;
#135568=CARTESIAN_POINT ( 'NONE',  ( 33.48921356237309510, -27.52281430457078670, 5.000000000000000000 ) ) ;
#135569=DIRECTION ( 'NONE',  ( 0.7071067811865486830, -0.7071067811865464625, -0.000000000000000000 ) ) ;
#135571=DIRECTION ( 'NONE',  ( -0.7071067811865486830, 0.7071067811865464625, 0.000000000000000000 ) ) ;
#135572=EDGE_CURVE ( 'NONE', #51152, #48040, #75163, .T. ) ;
#135573=EDGE_CURVE ( 'NONE', #44042, #114197, #130959, .T. ) ;
#135575=ORIENTED_EDGE ( 'NONE', *, *, #138109, .T. ) ;
#135578=ORIENTED_EDGE ( 'NONE', *, *, #118971, .T. ) ;
#135580=DIRECTION ( 'NONE',  ( 0.7071067811865486830, -0.7071067811865463515, 0.000000000000000000 ) ) ;
#135582=CARTESIAN_POINT ( 'NONE',  ( -29.51783344222318206, 22.22500000000000142, 7.048977539241911394 ) ) ;
#135583=ADVANCED_FACE ( 'NONE', ( #53369 ), #31632, .F. ) ;
#135585=LINE ( 'NONE', #14498, #4860 ) ;
#135587=ORIENTED_EDGE ( 'NONE', *, *, #111250, .T. ) ;
#135588=ORIENTED_EDGE ( 'NONE', *, *, #97333, .T. ) ;
#135589=DIRECTION ( 'NONE',  ( -0.6830127018922180770, -0.6830127018922204085, -0.2588190451025213501 ) ) ;
#135590=CARTESIAN_POINT ( 'NONE',  ( -34.00193056682073944, -22.22500000000000142, 4.500000000000000888 ) ) ;
#135591=EDGE_LOOP ( 'NONE', ( #127224, #121705, #18220, #63502 ) ) ;
#135593=ORIENTED_EDGE ( 'NONE', *, *, #5900, .T. ) ;
#135594=CARTESIAN_POINT ( 'NONE',  ( 2.999999999999988898, 8.966399257802175171, 5.000000000000000000 ) ) ;
#135595=DIRECTION ( 'NONE',  ( 0.6830127018922180770, -0.6830127018922204085, -0.2588190451025213501 ) ) ;
#135598=VERTEX_POINT ( 'NONE', #140380 ) ;
#135599=CARTESIAN_POINT ( 'NONE',  ( -34.92500000000001137, 22.22500000000000142, 4.000000000000000000 ) ) ;
#135600=EDGE_LOOP ( 'NONE', ( #54764, #37026, #14620, #65023 ) ) ;
#135601=EDGE_LOOP ( 'NONE', ( #86663, #18102, #100262, #60844 ) ) ;
#135602=PLANE ( 'NONE',  #772 ) ;
#135603=DIRECTION ( 'NONE',  ( 0.7071067811865487940, -0.7071067811865463515, -0.000000000000000000 ) ) ;
#135605=ORIENTED_EDGE ( 'NONE', *, *, #27646, .F. ) ;
#135606=DIRECTION ( 'NONE',  ( 0.7071067811865486830, -0.7071067811865464625, -0.000000000000000000 ) ) ;
#135607=CARTESIAN_POINT ( 'NONE',  ( 51.18398860626899705, 28.73617430169823095, 5.000000000000000000 ) ) ;
#135608=FACE_OUTER_BOUND ( 'NONE', #22899, .T. ) ;
#135609=DIRECTION ( 'NONE',  ( -0.6830127018922181881, 0.6830127018922202975, -0.2588190451025214056 ) ) ;
#135610=EDGE_CURVE ( 'NONE', #82851, #3366, #20732, .T. ) ;
#135611=FACE_BOUND ( 'NONE', #95836, .T. ) ;
#135612=VERTEX_POINT ( 'NONE', #41070 ) ;
#135613=DIRECTION ( 'NONE',  ( 0.7071067811865487940, 0.7071067811865463515, 0.000000000000000000 ) ) ;
#135614=EDGE_CURVE ( 'NONE', #30612, #27690, #131661, .T. ) ;
#135615=CARTESIAN_POINT ( 'NONE',  ( 24.18500016416798459, 22.22500000000000142, -17.39898871004312042 ) ) ;
#135616=LINE ( 'NONE', #105115, #63094 ) ;
#135617=ORIENTED_EDGE ( 'NONE', *, *, #102397, .T. ) ;
#135618=CARTESIAN_POINT ( 'NONE',  ( 16.49999999999988987, 18.43112307739199451, 4.000000000000000000 ) ) ;
#135619=VERTEX_POINT ( 'NONE', #42531 ) ;
#135620=ORIENTED_EDGE ( 'NONE', *, *, #24812, .T. ) ;
#135621=ORIENTED_EDGE ( 'NONE', *, *, #131313, .T. ) ;
#135622=EDGE_CURVE ( 'NONE', #134021, #48818, #29467, .T. ) ;
#135624=CIRCLE ( 'NONE', #29134, 5.968999999999998529 ) ;
#135626=ORIENTED_EDGE ( 'NONE', *, *, #25026, .F. ) ;
#135627=LINE ( 'NONE', #45787, #23233 ) ;
#135629=LINE ( 'NONE', #79137, #91418 ) ;
#135630=EDGE_CURVE ( 'NONE', #72508, #42487, #71601, .T. ) ;
#135631=VERTEX_POINT ( 'NONE', #107736 ) ;
#135632=DIRECTION ( 'NONE',  ( -0.7071067811865487940, 0.7071067811865463515, -0.000000000000000000 ) ) ;
#135634=EDGE_CURVE ( 'NONE', #73177, #32784, #62125, .T. ) ;
#135635=CARTESIAN_POINT ( 'NONE',  ( -4.828169399223495084, -11.24070752338417201, 4.000000000000000000 ) ) ;
#135636=LINE ( 'NONE', #124746, #143523 ) ;
#135637=LINE ( 'NONE', #15937, #18139 ) ;
#135638=CARTESIAN_POINT ( 'NONE',  ( 42.29974487139158157, -27.71228299555235708, 4.000000000000000000 ) ) ;
#135639=ORIENTED_EDGE ( 'NONE', *, *, #58465, .F. ) ;
#135640=ORIENTED_EDGE ( 'NONE', *, *, #84683, .T. ) ;
#135641=VERTEX_POINT ( 'NONE', #19319 ) ;
#135642=ORIENTED_EDGE ( 'NONE', *, *, #143322, .F. ) ;
#135643=CARTESIAN_POINT ( 'NONE',  ( 26.99999999999980815, 19.93112307739197675, 4.000000000000000000 ) ) ;
#135644=EDGE_CURVE ( 'NONE', #84525, #79859, #139704, .T. ) ;
#135645=ORIENTED_EDGE ( 'NONE', *, *, #57872, .F. ) ;
#135646=VERTEX_POINT ( 'NONE', #97580 ) ;
#135648=LINE ( 'NONE', #60988, #97190 ) ;
#135649=ORIENTED_EDGE ( 'NONE', *, *, #105617, .T. ) ;
#135651=ADVANCED_FACE ( 'NONE', ( #40386 ), #8397, .T. ) ;
#135654=CARTESIAN_POINT ( 'NONE',  ( 66.18398860626901126, 28.73617430169833753, 5.000000000000000000 ) ) ;
#135658=ORIENTED_EDGE ( 'NONE', *, *, #23566, .T. ) ;
#135660=DIRECTION ( 'NONE',  ( 0.7071067811865486830, -0.7071067811865464625, -0.000000000000000000 ) ) ;
#135661=VECTOR ( 'NONE', #121903, 1000.000000000000000 ) ;
#135664=PLANE ( 'NONE',  #55735 ) ;
#135665=ADVANCED_FACE ( 'NONE', ( #35222 ), #55532, .F. ) ;
#135666=ORIENTED_EDGE ( 'NONE', *, *, #11243, .T. ) ;
#135667=DIRECTION ( 'NONE',  ( -0.7071067811865486830, 0.7071067811865464625, 0.000000000000000000 ) ) ;
#135668=VERTEX_POINT ( 'NONE', #2532 ) ;
#135670=CARTESIAN_POINT ( 'NONE',  ( -39.18398860626899705, 28.73617430169814568, 5.000000000000000000 ) ) ;
#135671=AXIS2_PLACEMENT_3D ( 'NONE', #66019, #10856, #55123 ) ;
#135673=CARTESIAN_POINT ( 'NONE',  ( 0.000000000000000000, 21.72500000000000142, 4.500000000000000888 ) ) ;
#135674=CARTESIAN_POINT ( 'NONE',  ( -34.92500000000001137, 22.22500000000000142, 4.000000000000000000 ) ) ;
#135675=ORIENTED_EDGE ( 'NONE', *, *, #29172, .T. ) ;
#135676=EDGE_CURVE ( 'NONE', #91343, #139204, #1111, .T. ) ;
#135677=ADVANCED_FACE ( 'NONE', ( #35937 ), #132407, .T. ) ;
#135678=DIRECTION ( 'NONE',  ( -0.000000000000000000, -0.000000000000000000, 1.000000000000000000 ) ) ;
#135680=VERTEX_POINT ( 'NONE', #67116 ) ;
#135681=DIRECTION ( 'NONE',  ( -0.000000000000000000, 0.3543493200069153248, 0.9351131265310292928 ) ) ;
#135682=CARTESIAN_POINT ( 'NONE',  ( -39.48921356237310221, -27.52281430457082934, 5.000000000000000000 ) ) ;
#135683=ADVANCED_FACE ( 'NONE', ( #101152 ), #44691, .T. ) ;
#135684=ORIENTED_EDGE ( 'NONE', *, *, #100811, .F. ) ;
#135685=PLANE ( 'NONE',  #16264 ) ;
#135686=ORIENTED_EDGE ( 'NONE', *, *, #29011, .F. ) ;
#135687=ORIENTED_EDGE ( 'NONE', *, *, #116842, .F. ) ;
#135689=DIRECTION ( 'NONE',  ( -0.7071067811865486830, -0.7071067811865464625, 0.000000000000000000 ) ) ;
#135690=ORIENTED_EDGE ( 'NONE', *, *, #11070, .F. ) ;
#135691=DIRECTION ( 'NONE',  ( 0.7071067811865486830, -0.7071067811865464625, -0.000000000000000000 ) ) ;
#135692=LINE ( 'NONE', #124097, #9016 ) ;
#135694=ORIENTED_EDGE ( 'NONE', *, *, #19445, .F. ) ;
#135695=EDGE_CURVE ( 'NONE', #104041, #23176, #86430, .T. ) ;
#135696=CARTESIAN_POINT ( 'NONE',  ( -3.299744871391591339, -27.71228299555208352, 4.000000000000000000 ) ) ;
#135697=CARTESIAN_POINT ( 'NONE',  ( 3.707106781186514599, -9.740707523384186217, 5.000000000000000000 ) ) ;
#135698=LINE ( 'NONE', #124812, #33222 ) ;
#135699=CARTESIAN_POINT ( 'NONE',  ( 0.000000000000000000, 0.000000000000000000, 5.000000000000000000 ) ) ;
#135701=CARTESIAN_POINT ( 'NONE',  ( -39.18398860626899705, 28.73617430169814568, 5.000000000000000000 ) ) ;
#135702=ADVANCED_FACE ( 'NONE', ( #56977 ), #77308, .F. ) ;
#135703=DIRECTION ( 'NONE',  ( 0.7071067811865487940, 0.7071067811865463515, 0.000000000000000000 ) ) ;
#135704=CARTESIAN_POINT ( 'NONE',  ( -9.328169399223465774, 17.25929247661554555, 4.000000000000000000 ) ) ;
#135705=VERTEX_POINT ( 'NONE', #396 ) ;
#135706=ORIENTED_EDGE ( 'NONE', *, *, #53385, .F. ) ;
#135707=ORIENTED_EDGE ( 'NONE', *, *, #1244, .F. ) ;
#135709=ORIENTED_EDGE ( 'NONE', *, *, #19337, .T. ) ;
#135711=ORIENTED_EDGE ( 'NONE', *, *, #130264, .T. ) ;
#135714=ORIENTED_EDGE ( 'NONE', *, *, #19423, .F. ) ;
#135715=FACE_OUTER_BOUND ( 'NONE', #73821, .T. ) ;
#135716=CARTESIAN_POINT ( 'NONE',  ( 17.81601139373099940, 28.73617430169775133, 5.000000000000000000 ) ) ;
#135717=DIRECTION ( 'NONE',  ( -0.7071067811865486830, 0.7071067811865464625, 0.000000000000000000 ) ) ;
#135718=CARTESIAN_POINT ( 'NONE',  ( -19.49999999999986500, -10.91253812416064406, 4.000000000000000000 ) ) ;
#135720=EDGE_LOOP ( 'NONE', ( #46725, #104127, #39005, #44346 ) ) ;
#135721=DIRECTION ( 'NONE',  ( 0.7071067811865487940, 0.7071067811865463515, 0.000000000000000000 ) ) ;
#135722=CARTESIAN_POINT ( 'NONE',  ( 36.29974487139159578, -27.71228299555231445, 4.000000000000000000 ) ) ;
#135723=CARTESIAN_POINT ( 'NONE',  ( 15.18398860626900237, 28.73617430169797871, 5.000000000000000000 ) ) ;
#135725=DIRECTION ( 'NONE',  ( -0.6830127018922180770, -0.6830127018922204085, -0.2588190451025213501 ) ) ;
#135727=CARTESIAN_POINT ( 'NONE',  ( -7.499999999999947597, 18.43112307739200162, 4.000000000000000000 ) ) ;
#135731=DIRECTION ( 'NONE',  ( 0.7071067811865487940, 0.7071067811865463515, 0.000000000000000000 ) ) ;
#135733=DIRECTION ( 'NONE',  ( 0.7071067811865487940, 0.7071067811865463515, -0.000000000000000000 ) ) ;
#135734=VERTEX_POINT ( 'NONE', #121477 ) ;
#135735=EDGE_LOOP ( 'NONE', ( #107843, #123425, #105700, #86969 ) ) ;
#135737=ORIENTED_EDGE ( 'NONE', *, *, #88840, .F. ) ;
#135740=CARTESIAN_POINT ( 'NONE',  ( 9.707106781186482181, 8.259292476615627265, 5.000000000000000000 ) ) ;
#135741=DIRECTION ( 'NONE',  ( 0.7071067811865486830, -0.7071067811865464625, -0.000000000000000000 ) ) ;
#135743=DIRECTION ( 'NONE',  ( 0.6830127018922181881, 0.6830127018922202975, -0.2588190451025214056 ) ) ;
#135745=EDGE_CURVE ( 'NONE', #7189, #21579, #88884, .T. ) ;
#135747=VECTOR ( 'NONE', #133749, 1000.000000000000000 ) ;
#135748=ORIENTED_EDGE ( 'NONE', *, *, #134052, .F. ) ;
#135749=DIRECTION ( 'NONE',  ( -0.7071067811865486830, -0.7071067811865464625, 0.000000000000000000 ) ) ;
#135750=EDGE_LOOP ( 'NONE', ( #51201, #61174, #44380, #78887 ) ) ;
#135752=DIRECTION ( 'NONE',  ( -0.7071067811865486830, -0.7071067811865464625, -0.000000000000000000 ) ) ;
#135753=DIRECTION ( 'NONE',  ( -0.6830127018922180770, -0.6830127018922204085, -0.2588190451025213501 ) ) ;
#135755=ORIENTED_EDGE ( 'NONE', *, *, #65647, .T. ) ;
#135757=ADVANCED_FACE ( 'NONE', ( #133111 ), #68562, .T. ) ;
#135758=ORIENTED_EDGE ( 'NONE', *, *, #11063, .F. ) ;
#135760=LINE ( 'NONE', #47377, #127261 ) ;
#135761=LINE ( 'NONE', #39314, #121961 ) ;
#135762=CARTESIAN_POINT ( 'NONE',  ( -27.18398860626900060, 28.73617430169806042, 5.000000000000000000 ) ) ;
#135764=AXIS2_PLACEMENT_3D ( 'NONE', #105425, #3933, #127183 ) ;
#135765=AXIS2_PLACEMENT_3D ( 'NONE', #116667, #81949, #61613 ) ;
#135767=PLANE ( 'NONE',  #53440 ) ;
#135768=LINE ( 'NONE', #114007, #3767 ) ;
#135769=VERTEX_POINT ( 'NONE', #33789 ) ;
#135770=ORIENTED_EDGE ( 'NONE', *, *, #136620, .T. ) ;
#135771=CARTESIAN_POINT ( 'NONE',  ( -34.42500000000001137, 0.000000000000000000, 4.500000000000000888 ) ) ;
#135772=ORIENTED_EDGE ( 'NONE', *, *, #61525, .T. ) ;
#135773=CARTESIAN_POINT ( 'NONE',  ( 34.49999999999975131, -1.912538124160733766, 4.000000000000000000 ) ) ;
#135775=ORIENTED_EDGE ( 'NONE', *, *, #15479, .F. ) ;
#135776=CARTESIAN_POINT ( 'NONE',  ( 26.67183060077628554, -18.74070752338408852, 4.000000000000000000 ) ) ;
#135777=EDGE_CURVE ( 'NONE', #74246, #27583, #112749, .T. ) ;
#135778=DIRECTION ( 'NONE',  ( 0.7071067811865486830, -0.7071067811865464625, -0.000000000000000000 ) ) ;
#135779=CARTESIAN_POINT ( 'NONE',  ( 30.29974487139158867, -27.71228299555227537, 4.000000000000000000 ) ) ;
#135780=FACE_BOUND ( 'NONE', #130797, .T. ) ;
#135781=LINE ( 'NONE', #48783, #115078 ) ;
#135783=ADVANCED_FACE ( 'NONE', ( #103282 ), #27157, .F. ) ;
#135784=CARTESIAN_POINT ( 'NONE',  ( 1.734723475976807094E-15, 7.552185695429095347, 5.000000000000000000 ) ) ;
#135785=CARTESIAN_POINT ( 'NONE',  ( -15.48921356237309510, -27.52281430457066236, 5.000000000000000000 ) ) ;
#135787=ORIENTED_EDGE ( 'NONE', *, *, #85932, .T. ) ;
#135788=LINE ( 'NONE', #13979, #42520 ) ;
#135789=ORIENTED_EDGE ( 'NONE', *, *, #142426, .T. ) ;
#135790=ADVANCED_FACE ( 'NONE', ( #94545 ), #126462, .F. ) ;
#135792=ORIENTED_EDGE ( 'NONE', *, *, #15546, .F. ) ;
#135794=EDGE_LOOP ( 'NONE', ( #139564, #107738, #48290, #130860 ) ) ;
#135796=LINE ( 'NONE', #3797, #118118 ) ;
#135797=EDGE_CURVE ( 'NONE', #23925, #25963, #71399, .T. ) ;
#135800=ADVANCED_FACE ( 'NONE', ( #49670 ), #82287, .F. ) ;
#135801=CARTESIAN_POINT ( 'NONE',  ( -24.48921356237309510, -27.52281430457072631, 5.000000000000000000 ) ) ;
#135802=EDGE_CURVE ( 'NONE', #72918, #59821, #115558, .T. ) ;
#135803=DIRECTION ( 'NONE',  ( -0.7071067811865486830, 0.7071067811865464625, 0.000000000000000000 ) ) ;
#135804=LINE ( 'NONE', #55402, #143158 ) ;
#135805=DIRECTION ( 'NONE',  ( -0.000000000000000000, -0.3543493200069152693, 0.9351131265310292928 ) ) ;
#135807=CARTESIAN_POINT ( 'NONE',  ( 36.48921356237310221, -27.52281430457080802, 5.000000000000000000 ) ) ;
#135810=AXIS2_PLACEMENT_3D ( 'NONE', #20674, #31575, #10506 ) ;
#135812=DIRECTION ( 'NONE',  ( 0.000000000000000000, -0.3543493200069152138, 0.9351131265310292928 ) ) ;
#135813=FACE_OUTER_BOUND ( 'NONE', #141812, .T. ) ;
#135814=ORIENTED_EDGE ( 'NONE', *, *, #130827, .F. ) ;
#135815=ADVANCED_FACE ( 'NONE', ( #136630 ), #92403, .F. ) ;
#135816=ORIENTED_EDGE ( 'NONE', *, *, #59479, .F. ) ;
#135817=VERTEX_POINT ( 'NONE', #16248 ) ;
#135818=DIRECTION ( 'NONE',  ( 0.7071067811865487940, 0.7071067811865463515, 0.000000000000000000 ) ) ;
#135819=ORIENTED_EDGE ( 'NONE', *, *, #23716, .T. ) ;
#135820=PLANE ( 'NONE',  #106468 ) ;
#135822=AXIS2_PLACEMENT_3D ( 'NONE', #96535, #41466, #7399 ) ;
#135823=CARTESIAN_POINT ( 'NONE',  ( -7.265066702820462297, 12.75929247661558996, 18.34774599283958096 ) ) ;
#135825=CARTESIAN_POINT ( 'NONE',  ( 48.18398860626899705, 28.73617430169820608, 5.000000000000000000 ) ) ;
#135826=VERTEX_POINT ( 'NONE', #25735 ) ;
#135827=VECTOR ( 'NONE', #122936, 1000.000000000000000 ) ;
#135828=CARTESIAN_POINT ( 'NONE',  ( -45.48921356237309510, -27.52281430457087197, 5.000000000000000000 ) ) ;
#135829=DIRECTION ( 'NONE',  ( 0.7071067811865487940, 0.7071067811865463515, 0.000000000000000000 ) ) ;
#135830=DIRECTION ( 'NONE',  ( 0.6830127018922181881, 0.6830127018922202975, -0.2588190451025214056 ) ) ;
#135831=ORIENTED_EDGE ( 'NONE', *, *, #90256, .F. ) ;
#135832=VERTEX_POINT ( 'NONE', #14136 ) ;
#135833=CARTESIAN_POINT ( 'NONE',  ( -60.48921356237309510, -27.52281430457097500, 5.000000000000000000 ) ) ;
#135835=LINE ( 'NONE', #36521, #102647 ) ;
#135836=EDGE_LOOP ( 'NONE', ( #12204, #9726, #31456, #138561 ) ) ;
#135840=VECTOR ( 'NONE', #7737, 1000.000000000000000 ) ;
#135841=EDGE_CURVE ( 'NONE', #26904, #117439, #59814, .T. ) ;
#135842=DIRECTION ( 'NONE',  ( -0.6830127018922180770, -0.6830127018922204085, -0.2588190451025213501 ) ) ;
#135843=CARTESIAN_POINT ( 'NONE',  ( -19.49999999999985789, -19.91253812416055524, 4.000000000000000000 ) ) ;
#135844=CARTESIAN_POINT ( 'NONE',  ( 1.980122250714512422, -17.24070752338410273, 20.23474786156469918 ) ) ;
#135845=EDGE_LOOP ( 'NONE', ( #10412, #80136, #57496, #61840 ) ) ;
#135846=CARTESIAN_POINT ( 'NONE',  ( 11.99999999999992362, -3.033600742197707145, 5.000000000000000000 ) ) ;
#135847=FACE_OUTER_BOUND ( 'NONE', #59600, .T. ) ;
#135849=CARTESIAN_POINT ( 'NONE',  ( -54.18398860626899705, 28.73617430169825226, 5.000000000000000000 ) ) ;
#135850=DIRECTION ( 'NONE',  ( -0.7071067811865487940, 0.7071067811865463515, -0.000000000000000000 ) ) ;
#135851=AXIS2_PLACEMENT_3D ( 'NONE', #60549, #48210, #115559 ) ;
#135852=DIRECTION ( 'NONE',  ( 0.3543493200069162685, -0.000000000000000000, -0.9351131265310288487 ) ) ;
#135853=ORIENTED_EDGE ( 'NONE', *, *, #25652, .F. ) ;
#135854=VERTEX_POINT ( 'NONE', #63407 ) ;
#135855=CARTESIAN_POINT ( 'NONE',  ( -26.99999999999981526, -1.068876922607802538, 4.000000000000000000 ) ) ;
#135856=CARTESIAN_POINT ( 'NONE',  ( 6.707106781186496391, -18.74070752338408852, 5.000000000000000000 ) ) ;
#135857=CIRCLE ( 'NONE', #96491, 5.968999999999998529 ) ;
#135860=DIRECTION ( 'NONE',  ( 0.7071067811865487940, 0.7071067811865463515, 0.000000000000000000 ) ) ;
#135861=VECTOR ( 'NONE', #134680, 1000.000000000000227 ) ;
#135862=DIRECTION ( 'NONE',  ( 0.6830127018922181881, 0.6830127018922202975, -0.2588190451025214056 ) ) ;
#135863=LINE ( 'NONE', #90204, #39095 ) ;
#135865=ORIENTED_EDGE ( 'NONE', *, *, #76566, .T. ) ;
#135867=CARTESIAN_POINT ( 'NONE',  ( 68.99451991528748351, 28.92564299267986172, 4.000000000000000000 ) ) ;
#135868=VECTOR ( 'NONE', #95076, 1000.000000000000000 ) ;
#135869=DIRECTION ( 'NONE',  ( -0.6830127018922180770, -0.6830127018922204085, -0.2588190451025213501 ) ) ;
#135871=CARTESIAN_POINT ( 'NONE',  ( -2.671830600776445852, 11.25929247661560240, 4.000000000000000000 ) ) ;
#135872=CARTESIAN_POINT ( 'NONE',  ( 0.000000000000000000, 0.000000000000000000, 5.000000000000000000 ) ) ;
#135873=EDGE_LOOP ( 'NONE', ( #26536, #129993, #131374, #55974 ) ) ;
#135875=ORIENTED_EDGE ( 'NONE', *, *, #135486, .F. ) ;
#135876=DIRECTION ( 'NONE',  ( -0.7071067811865487940, 0.7071067811865463515, 0.000000000000000000 ) ) ;
#135877=DIRECTION ( 'NONE',  ( -0.7071067811865487940, 0.7071067811865463515, 0.000000000000000000 ) ) ;
#135878=PLANE ( 'NONE',  #28000 ) ;
#135879=CARTESIAN_POINT ( 'NONE',  ( -57.29974487139158157, -27.71228299555246011, 4.000000000000000000 ) ) ;
#135880=EDGE_CURVE ( 'NONE', #126258, #71524, #130897, .T. ) ;
#135881=DIRECTION ( 'NONE',  ( -1.000000000000000000, 0.000000000000000000, 0.000000000000000000 ) ) ;
#135883=VERTEX_POINT ( 'NONE', #7535 ) ;
#135884=EDGE_CURVE ( 'NONE', #94958, #82809, #97390, .T. ) ;
#135886=CARTESIAN_POINT ( 'NONE',  ( 34.92499999999998295, 0.7592924766157138627, 4.255531930566151644 ) ) ;
#135887=CARTESIAN_POINT ( 'NONE',  ( -14.75830541574804222, 0.7592924766157138627, 14.37146558664986351 ) ) ;
#135888=VECTOR ( 'NONE', #137434, 1000.000000000000000 ) ;
#135889=DIRECTION ( 'NONE',  ( 1.000000000000000000, 0.000000000000000000, 0.000000000000000000 ) ) ;
#135890=DIRECTION ( 'NONE',  ( -0.3543493200069162685, -0.000000000000000000, -0.9351131265310288487 ) ) ;
#135892=EDGE_CURVE ( 'NONE', #53838, #72096, #86564, .T. ) ;
#135893=VECTOR ( 'NONE', #72869, 1000.000000000000000 ) ;
#135894=CARTESIAN_POINT ( 'NONE',  ( 26.99999999999981526, -0.4125381241607464222, 4.000000000000000000 ) ) ;
#135895=ORIENTED_EDGE ( 'NONE', *, *, #118722, .F. ) ;
#135897=LINE ( 'NONE', #58393, #134979 ) ;
#135898=LINE ( 'NONE', #79432, #48542 ) ;
#135899=LINE ( 'NONE', #113416, #84553 ) ;
#135901=ORIENTED_EDGE ( 'NONE', *, *, #72676, .T. ) ;
#135902=EDGE_CURVE ( 'NONE', #70329, #110682, #129320, .T. ) ;
#135903=DIRECTION ( 'NONE',  ( 0.6830127018922180770, -0.6830127018922204085, -0.2588190451025213501 ) ) ;
#135904=EDGE_CURVE ( 'NONE', #67554, #28495, #108984, .T. ) ;
#135905=LINE ( 'NONE', #89540, #139361 ) ;
#135908=FACE_OUTER_BOUND ( 'NONE', #45556, .T. ) ;
#135909=ORIENTED_EDGE ( 'NONE', *, *, #12967, .F. ) ;
#135910=ORIENTED_EDGE ( 'NONE', *, *, #10969, .F. ) ;
#135911=DIRECTION ( 'NONE',  ( -0.6830127018922181881, 0.6830127018922202975, -0.2588190451025214056 ) ) ;
#135912=LINE ( 'NONE', #91688, #81435 ) ;
#135913=AXIS2_PLACEMENT_3D ( 'NONE', #110952, #100124, #67517 ) ;
#135915=EDGE_CURVE ( 'NONE', #38500, #61103, #18396, .T. ) ;
#135916=LINE ( 'NONE', #101134, #88166 ) ;
#135917=DIRECTION ( 'NONE',  ( 0.7071067811865487940, 0.7071067811865463515, 0.000000000000000000 ) ) ;
#135918=EDGE_LOOP ( 'NONE', ( #84121, #7586, #41708 ) ) ;
#135919=DIRECTION ( 'NONE',  ( 0.6830127018922181881, 0.6830127018922202975, -0.2588190451025214056 ) ) ;
#135920=FACE_OUTER_BOUND ( 'NONE', #16216, .T. ) ;
#135922=EDGE_LOOP ( 'NONE', ( #135341, #42121, #6051, #33889 ) ) ;
#135923=VERTEX_POINT ( 'NONE', #28618 ) ;
#135924=VECTOR ( 'NONE', #134368, 1000.000000000000000 ) ;
#135925=DIRECTION ( 'NONE',  ( 1.000000000000000000, 0.000000000000000000, 0.000000000000000000 ) ) ;
#135927=CARTESIAN_POINT ( 'NONE',  ( 42.29974487139158157, -27.71228299555235708, 4.000000000000000000 ) ) ;
#135930=FACE_OUTER_BOUND ( 'NONE', #122944, .T. ) ;
#135931=ORIENTED_EDGE ( 'NONE', *, *, #140388, .F. ) ;
#135933=FACE_OUTER_BOUND ( 'NONE', #76446, .T. ) ;
#135934=ORIENTED_EDGE ( 'NONE', *, *, #107749, .T. ) ;
#135935=DIRECTION ( 'NONE',  ( -0.3543493200069162685, -0.000000000000000000, -0.9351131265310288487 ) ) ;
#135936=ORIENTED_EDGE ( 'NONE', *, *, #94098, .F. ) ;
#135937=FACE_OUTER_BOUND ( 'NONE', #116647, .T. ) ;
#135938=LINE ( 'NONE', #101162, #102589 ) ;
#135939=EDGE_LOOP ( 'NONE', ( #45978, #6274, #73108, #61914 ) ) ;
#135940=VECTOR ( 'NONE', #52826, 1000.000000000000227 ) ;
#135941=FACE_BOUND ( 'NONE', #52331, .T. ) ;
#135942=DIRECTION ( 'NONE',  ( -0.000000000000000000, -0.3543493200069152693, 0.9351131265310292928 ) ) ;
#135943=EDGE_CURVE ( 'NONE', #126702, #6455, #62666, .T. ) ;
#135944=DIRECTION ( 'NONE',  ( 0.7071067811865486830, -0.7071067811865464625, -0.000000000000000000 ) ) ;
#135945=LINE ( 'NONE', #45407, #85313 ) ;
#135946=CARTESIAN_POINT ( 'NONE',  ( 15.18398860626900237, 28.73617430169797871, 5.000000000000000000 ) ) ;
#135947=VECTOR ( 'NONE', #4646, 999.9999999999998863 ) ;
#135949=DIRECTION ( 'NONE',  ( -0.7071067811865486830, -0.7071067811865464625, 0.000000000000000000 ) ) ;
#135951=ORIENTED_EDGE ( 'NONE', *, *, #58289, .T. ) ;
#135953=EDGE_CURVE ( 'NONE', #38622, #85582, #130796, .T. ) ;
#135954=ORIENTED_EDGE ( 'NONE', *, *, #24514, .F. ) ;
#135957=EDGE_CURVE ( 'NONE', #22428, #70976, #96663, .T. ) ;
#135958=CARTESIAN_POINT ( 'NONE',  ( 28.17183060077627133, 0.7592924766157069794, 4.000000000000000000 ) ) ;
#135959=ADVANCED_FACE ( 'NONE', ( #19847 ), #53950, .F. ) ;
#135960=VECTOR ( 'NONE', #59297, 1000.000000000000000 ) ;
#135961=LINE ( 'NONE', #93170, #699 ) ;
#135964=DIRECTION ( 'NONE',  ( -0.7071067811865487940, 0.7071067811865463515, -0.000000000000000000 ) ) ;
#135965=ORIENTED_EDGE ( 'NONE', *, *, #135201, .T. ) ;
#135968=EDGE_CURVE ( 'NONE', #36236, #89986, #2112, .T. ) ;
#135969=CARTESIAN_POINT ( 'NONE',  ( 26.99451991528749417, 28.92564299267956685, 4.000000000000000000 ) ) ;
#135971=CARTESIAN_POINT ( 'NONE',  ( -3.489213562373097322, -27.52281430457057709, 5.000000000000000000 ) ) ;
#135972=CARTESIAN_POINT ( 'NONE',  ( -8.292893218813391698, 5.259292476615661016, 5.000000000000000000 ) ) ;
#135973=VERTEX_POINT ( 'NONE', #41607 ) ;
#135975=( BOUNDED_CURVE ( )  B_SPLINE_CURVE ( 3, ( #52636, #11250, #64247, #20720 ),
 .UNSPECIFIED., .F., .F. ) 
 B_SPLINE_CURVE_WITH_KNOTS ( ( 4, 4 ),
 ( 1.502886732431669481, 1.547827028402603888 ),
 .UNSPECIFIED. ) 
 CURVE ( )  GEOMETRIC_REPRESENTATION_ITEM ( )  RATIONAL_B_SPLINE_CURVE ( ( 1.000000000000000000, 0.9998317045644854462, 0.9998317045644854462, 1.000000000000000000 ) ) 
 REPRESENTATION_ITEM ( '' )  );
#135976=DIRECTION ( 'NONE',  ( 0.3543493200069162685, -0.000000000000000000, -0.9351131265310288487 ) ) ;
#135977=EDGE_CURVE ( 'NONE', #70558, #89696, #106855, .T. ) ;
#135978=ORIENTED_EDGE ( 'NONE', *, *, #34402, .T. ) ;
#135979=VERTEX_POINT ( 'NONE', #106119 ) ;
#135980=EDGE_CURVE ( 'NONE', #86031, #37037, #64083, .T. ) ;
#135981=ORIENTED_EDGE ( 'NONE', *, *, #32566, .F. ) ;
#135983=VECTOR ( 'NONE', #67753, 1000.000000000000000 ) ;
#135984=VERTEX_POINT ( 'NONE', #53190 ) ;
#135985=ADVANCED_FACE ( 'NONE', ( #108252 ), #40906, .F. ) ;
#135987=CARTESIAN_POINT ( 'NONE',  ( -23.18650864602347283, -15.74070752338412049, 8.904080028138995573 ) ) ;
#135988=ORIENTED_EDGE ( 'NONE', *, *, #6623, .F. ) ;
#135990=ORIENTED_EDGE ( 'NONE', *, *, #1250, .F. ) ;
#135991=DIRECTION ( 'NONE',  ( -0.6830127018922180770, -0.6830127018922204085, -0.2588190451025213501 ) ) ;
#135992=VECTOR ( 'NONE', #80153, 1000.000000000000000 ) ;
#135993=CARTESIAN_POINT ( 'NONE',  ( -3.792893218813425893, -11.24070752338417201, 5.000000000000000000 ) ) ;
#135994=ORIENTED_EDGE ( 'NONE', *, *, #126388, .T. ) ;
#135995=ORIENTED_EDGE ( 'NONE', *, *, #59661, .F. ) ;
#135996=DIRECTION ( 'NONE',  ( -0.6830127018922180770, -0.6830127018922204085, -0.2588190451025213501 ) ) ;
#135997=CARTESIAN_POINT ( 'NONE',  ( 10.82816939922344979, 6.759292476615649470, 4.000000000000000000 ) ) ;
#135999=ORIENTED_EDGE ( 'NONE', *, *, #138941, .T. ) ;
#136000=PLANE ( 'NONE',  #66718 ) ;
#136001=ORIENTED_EDGE ( 'NONE', *, *, #101235, .F. ) ;
#136002=ORIENTED_EDGE ( 'NONE', *, *, #16856, .F. ) ;
#136004=EDGE_CURVE ( 'NONE', #23245, #98043, #34309, .T. ) ;
#136005=AXIS2_PLACEMENT_3D ( 'NONE', #74576, #129636, #31770 ) ;
#136006=LINE ( 'NONE', #114928, #120941 ) ;
#136007=CARTESIAN_POINT ( 'NONE',  ( -30.29974487139158867, -27.71228299555227537, 4.000000000000000000 ) ) ;
#136008=LINE ( 'NONE', #12784, #41642 ) ;
#136009=CARTESIAN_POINT ( 'NONE',  ( -15.18398860626900237, 28.73617430169797871, 5.000000000000000000 ) ) ;
#136010=EDGE_LOOP ( 'NONE', ( #132617, #130068, #12069, #112930 ) ) ;
#136011=LINE ( 'NONE', #12081, #121157 ) ;
#136012=ADVANCED_FACE ( 'NONE', ( #56098 ), #111878, .F. ) ;
#136014=CARTESIAN_POINT ( 'NONE',  ( -3.712309939660258795, -21.73547319004781286, 4.999917730833664642 ) ) ;
#136015=CARTESIAN_POINT ( 'NONE',  ( -42.29974487139158157, -27.71228299555235708, 4.000000000000000000 ) ) ;
#136016=AXIS2_PLACEMENT_3D ( 'NONE', #136309, #83376, #38441 ) ;
#136017=ORIENTED_EDGE ( 'NONE', *, *, #90893, .F. ) ;
#136018=ORIENTED_EDGE ( 'NONE', *, *, #53785, .F. ) ;
#136019=EDGE_CURVE ( 'NONE', #47990, #123098, #133632, .T. ) ;
#136020=VERTEX_POINT ( 'NONE', #111124 ) ;
#136021=CARTESIAN_POINT ( 'NONE',  ( -56.99451991528749062, 28.92564299267978001, 4.000000000000000000 ) ) ;
#136022=DIRECTION ( 'NONE',  ( -0.7071067811865486830, 0.7071067811865464625, 0.000000000000000000 ) ) ;
#136024=PLANE ( 'NONE',  #135350 ) ;
#136025=CARTESIAN_POINT ( 'NONE',  ( 34.49999999999975842, -11.94567065516892512, 4.994342998332160555 ) ) ;
#136026=LINE ( 'NONE', #48308, #70997 ) ;
#136028=CARTESIAN_POINT ( 'NONE',  ( -4.499999999999960920, 1.087461875839230707, 4.000000000000000000 ) ) ;
#136029=AXIS2_PLACEMENT_3D ( 'NONE', #80815, #102569, #70669 ) ;
#136030=LINE ( 'NONE', #92511, #30213 ) ;
#136031=EDGE_CURVE ( 'NONE', #67930, #62339, #87264, .T. ) ;
#136032=DIRECTION ( 'NONE',  ( -0.7071067811865486830, -0.7071067811865464625, -0.000000000000000000 ) ) ;
#136033=CARTESIAN_POINT ( 'NONE',  ( -10.49999999999992362, -15.29013452822855079, 0.3645803511610097303 ) ) ;
#136034=CARTESIAN_POINT ( 'NONE',  ( 34.92499999999998295, -13.29806943317888468, 4.500000000000000888 ) ) ;
#136035=VERTEX_POINT ( 'NONE', #87973 ) ;
#136037=ORIENTED_EDGE ( 'NONE', *, *, #98796, .T. ) ;
#136039=CARTESIAN_POINT ( 'NONE',  ( 8.816011393731004731, 28.73617430169781173, 5.000000000000000000 ) ) ;
#136040=CARTESIAN_POINT ( 'NONE',  ( 6.299744871391586898, -27.71228299555210484, 4.000000000000000000 ) ) ;
#136042=VECTOR ( 'NONE', #41089, 1000.000000000000000 ) ;
#136044=LINE ( 'NONE', #34600, #30140 ) ;
#136045=DIRECTION ( 'NONE',  ( -0.000000000000000000, 0.000000000000000000, 1.000000000000000000 ) ) ;
#136046=EDGE_LOOP ( 'NONE', ( #10503, #74893, #54384, #31617 ) ) ;
#136048=ORIENTED_EDGE ( 'NONE', *, *, #96662, .T. ) ;
#136049=DIRECTION ( 'NONE',  ( 0.7071067811865487940, 0.7071067811865463515, 0.000000000000000000 ) ) ;
#136050=EDGE_LOOP ( 'NONE', ( #110932, #33282, #23552, #132091 ) ) ;
#136051=VECTOR ( 'NONE', #65929, 1000.000000000000227 ) ;
#136052=VECTOR ( 'NONE', #123514, 1000.000000000000000 ) ;
#136053=LINE ( 'NONE', #27277, #1288 ) ;
#136055=DIRECTION ( 'NONE',  ( 0.3543493200069162685, -0.000000000000000000, -0.9351131265310288487 ) ) ;
#136058=FACE_OUTER_BOUND ( 'NONE', #73470, .T. ) ;
#136059=CARTESIAN_POINT ( 'NONE',  ( -30.28001967989385435, 0.7592924766157104211, 14.27032725228001908 ) ) ;
#136062=LINE ( 'NONE', #91838, #141708 ) ;
#136063=VECTOR ( 'NONE', #38762, 1000.000000000000000 ) ;
#136064=DIRECTION ( 'NONE',  ( -0.6830127018922181881, 0.6830127018922202975, -0.2588190451025214056 ) ) ;
#136065=FACE_OUTER_BOUND ( 'NONE', #30316, .T. ) ;
#136066=ORIENTED_EDGE ( 'NONE', *, *, #141858, .F. ) ;
#136069=EDGE_CURVE ( 'NONE', #69099, #72014, #131485, .T. ) ;
#136071=DIRECTION ( 'NONE',  ( -0.6830127018922180770, -0.6830127018922204085, -0.2588190451025213501 ) ) ;
#136072=FACE_OUTER_BOUND ( 'NONE', #51297, .T. ) ;
#136073=CARTESIAN_POINT ( 'NONE',  ( 34.49999999999975842, 19.46425560840029689, 4.994342998332160555 ) ) ;
#136074=DIRECTION ( 'NONE',  ( -0.000000000000000000, 0.000000000000000000, 1.000000000000000000 ) ) ;
#136075=EDGE_LOOP ( 'NONE', ( #102007, #66503, #79969, #116776 ) ) ;
#136076=CARTESIAN_POINT ( 'NONE',  ( -0.4892135623730947680, -27.52281430457055578, 5.000000000000000000 ) ) ;
#136077=CARTESIAN_POINT ( 'NONE',  ( 19.05000000000000071, 3.174999999999997158, 4.000000000000000000 ) ) ;
#136078=EDGE_CURVE ( 'NONE', #81070, #140110, #32913, .T. ) ;
#136079=VERTEX_POINT ( 'NONE', #77134 ) ;
#136081=ADVANCED_FACE ( 'NONE', ( #121307 ), #940, .F. ) ;
#136083=CARTESIAN_POINT ( 'NONE',  ( -54.29974487139159578, -27.71228299555243879, 4.000000000000000000 ) ) ;
#136084=VERTEX_POINT ( 'NONE', #57512 ) ;
#136085=DIRECTION ( 'NONE',  ( 0.6830127018922180770, -0.6830127018922204085, -0.2588190451025213501 ) ) ;
#136087=DIRECTION ( 'NONE',  ( 0.7071067811865487940, -0.7071067811865463515, 0.000000000000000000 ) ) ;
#136088=LINE ( 'NONE', #100620, #56271 ) ;
#136089=VERTEX_POINT ( 'NONE', #142372 ) ;
#136090=ORIENTED_EDGE ( 'NONE', *, *, #102895, .F. ) ;
#136093=( BOUNDED_CURVE ( )  B_SPLINE_CURVE ( 3, ( #36880, #26028, #137655, #70972 ),
 .UNSPECIFIED., .F., .T. ) 
 B_SPLINE_CURVE_WITH_KNOTS ( ( 4, 4 ),
 ( 5.920967161967926273, 7.341195215986589417 ),
 .UNSPECIFIED. ) 
 CURVE ( )  GEOMETRIC_REPRESENTATION_ITEM ( )  RATIONAL_B_SPLINE_CURVE ( ( 1.000000000000000000, 0.8388583629366715977, 0.8388583629366715977, 1.000000000000000000 ) ) 
 REPRESENTATION_ITEM ( '' )  );
#136094=ORIENTED_EDGE ( 'NONE', *, *, #115738, .F. ) ;
#136095=CARTESIAN_POINT ( 'NONE',  ( -30.48921356237309510, -27.52281430457076894, 5.000000000000000000 ) ) ;
#136096=LINE ( 'NONE', #125228, #96532 ) ;
#136100=EDGE_CURVE ( 'NONE', #47525, #91556, #110413, .T. ) ;
#136101=DIRECTION ( 'NONE',  ( 0.7071067811865487940, 0.7071067811865463515, -0.000000000000000000 ) ) ;
#136102=CARTESIAN_POINT ( 'NONE',  ( 24.79289321881329045, -14.24070752338413293, 5.000000000000000000 ) ) ;
#136103=DIRECTION ( 'NONE',  ( -0.7071067811865487940, 0.7071067811865463515, 0.000000000000000000 ) ) ;
#136105=ORIENTED_EDGE ( 'NONE', *, *, #101538, .T. ) ;
#136106=CARTESIAN_POINT ( 'NONE',  ( 48.18398860626899705, 28.73617430169820608, 5.000000000000000000 ) ) ;
#136107=DIRECTION ( 'NONE',  ( 0.7071067811865487940, 0.7071067811865463515, -0.000000000000000000 ) ) ;
#136108=DIRECTION ( 'NONE',  ( -0.000000000000000000, 0.3543493200069153248, 0.9351131265310292928 ) ) ;
#136109=VERTEX_POINT ( 'NONE', #89402 ) ;
#136110=VERTEX_POINT ( 'NONE', #11088 ) ;
#136111=DIRECTION ( 'NONE',  ( 0.7071067811865487940, -0.7071067811865463515, 0.000000000000000000 ) ) ;
#136112=CARTESIAN_POINT ( 'NONE',  ( -14.56319896779161027, -12.74070752338414891, 9.898150129686410281 ) ) ;
#136114=DIRECTION ( 'NONE',  ( 0.7071067811865487940, 0.7071067811865463515, 0.000000000000000000 ) ) ;
#136115=CARTESIAN_POINT ( 'NONE',  ( -74.99451991528749772, 28.92564299267990435, 4.000000000000000000 ) ) ;
#136116=FACE_OUTER_BOUND ( 'NONE', #8, .T. ) ;
#136117=DIRECTION ( 'NONE',  ( 1.000000000000000000, 0.000000000000000000, 0.000000000000000000 ) ) ;
#136119=EDGE_CURVE ( 'NONE', #43341, #88152, #35048, .T. ) ;
#136120=ORIENTED_EDGE ( 'NONE', *, *, #46362, .T. ) ;
#136123=EDGE_CURVE ( 'NONE', #109497, #142960, #99537, .T. ) ;
#136124=LINE ( 'NONE', #34690, #119776 ) ;
#136125=ORIENTED_EDGE ( 'NONE', *, *, #123353, .F. ) ;
#136126=ADVANCED_FACE ( 'NONE', ( #78534 ), #122738, .F. ) ;
#136127=ADVANCED_FACE ( 'NONE', ( #23416 ), #100983, .F. ) ;
#136129=DIRECTION ( 'NONE',  ( 0.7071067811865487940, 0.7071067811865463515, 0.000000000000000000 ) ) ;
#136130=ORIENTED_EDGE ( 'NONE', *, *, #85700, .T. ) ;
#136131=LINE ( 'NONE', #100668, #15843 ) ;
#136132=CARTESIAN_POINT ( 'NONE',  ( -39.48921356237310221, -27.52281430457082934, 5.000000000000000000 ) ) ;
#136133=CARTESIAN_POINT ( 'NONE',  ( -5.395137668124758257, 21.75929247661549937, 21.32995629748187838 ) ) ;
#136134=CARTESIAN_POINT ( 'NONE',  ( 16.82816939922340893, -17.24070752338411339, 4.000000000000000000 ) ) ;
#136135=VECTOR ( 'NONE', #62038, 1000.000000000000000 ) ;
#136136=PLANE ( 'NONE',  #465 ) ;
#136137=ORIENTED_EDGE ( 'NONE', *, *, #28998, .T. ) ;
#136138=LINE ( 'NONE', #98686, #72658 ) ;
#136139=DIRECTION ( 'NONE',  ( -0.6830127018922181881, 0.6830127018922202975, -0.2588190451025214056 ) ) ;
#136140=AXIS2_PLACEMENT_3D ( 'NONE', #142393, #121325, #118469 ) ;
#136141=EDGE_CURVE ( 'NONE', #119333, #91761, #1638, .T. ) ;
#136142=ORIENTED_EDGE ( 'NONE', *, *, #74970, .T. ) ;
#136144=ORIENTED_EDGE ( 'NONE', *, *, #131777, .T. ) ;
#136145=EDGE_CURVE ( 'NONE', #48159, #3321, #45920, .T. ) ;
#136146=EDGE_LOOP ( 'NONE', ( #84603, #103547, #70695, #52100 ) ) ;
#136147=CARTESIAN_POINT ( 'NONE',  ( -9.524001385854420576, 22.03583458319438648, 4.979811245910087614 ) ) ;
#136148=ORIENTED_EDGE ( 'NONE', *, *, #96849, .F. ) ;
#136149=ORIENTED_EDGE ( 'NONE', *, *, #84128, .F. ) ;
#136151=ORIENTED_EDGE ( 'NONE', *, *, #56657, .T. ) ;
#136153=AXIS2_PLACEMENT_3D ( 'NONE', #27655, #39275, #70515 ) ;
#136154=ADVANCED_FACE ( 'NONE', ( #134350 ), #79291, .T. ) ;
#136155=CARTESIAN_POINT ( 'NONE',  ( 23.89661266223020419, -0.3091507863911187037, 4.000000000000000000 ) ) ;
#136156=DIRECTION ( 'NONE',  ( 0.7071067811865487940, 0.7071067811865463515, -0.000000000000000000 ) ) ;
#136158=PLANE ( 'NONE',  #33294 ) ;
#136159=CARTESIAN_POINT ( 'NONE',  ( 24.69524342170288023, 1.235879655689124501, 4.000000000000000000 ) ) ;
#136160=CARTESIAN_POINT ( 'NONE',  ( -34.92500000000001137, 21.73644205237997795, 4.195230610814792094 ) ) ;
#136162=ADVANCED_FACE ( 'NONE', ( #4458 ), #15371, .F. ) ;
#136164=PLANE ( 'NONE',  #16582 ) ;
#136166=ORIENTED_EDGE ( 'NONE', *, *, #80033, .F. ) ;
#136168=LINE ( 'NONE', #81099, #38392 ) ;
#136169=ORIENTED_EDGE ( 'NONE', *, *, #92507, .F. ) ;
#136170=VERTEX_POINT ( 'NONE', #113279 ) ;
#136171=EDGE_CURVE ( 'NONE', #72085, #134621, #48766, .T. ) ;
#136172=DIRECTION ( 'NONE',  ( -0.000000000000000000, 0.3543493200069153248, 0.9351131265310292928 ) ) ;
#136173=ORIENTED_EDGE ( 'NONE', *, *, #131134, .F. ) ;
#136175=LINE ( 'NONE', #26704, #130178 ) ;
#136176=LINE ( 'NONE', #69524, #17688 ) ;
#136177=LINE ( 'NONE', #12250, #8546 ) ;
#136178=CARTESIAN_POINT ( 'NONE',  ( -62.99451991528749772, 28.92564299267982264, 4.000000000000000000 ) ) ;
#136179=CARTESIAN_POINT ( 'NONE',  ( -20.99451991528748707, 28.92564299267952777, 4.000000000000000000 ) ) ;
#136180=ORIENTED_EDGE ( 'NONE', *, *, #41124, .F. ) ;
#136181=VECTOR ( 'NONE', #109411, 1000.000000000000000 ) ;
#136182=CARTESIAN_POINT ( 'NONE',  ( -8.510786437626906675, -27.52281430457049183, 5.000000000000000000 ) ) ;
#136184=CARTESIAN_POINT ( 'NONE',  ( 39.48921356237310221, -27.52281430457082934, 5.000000000000000000 ) ) ;
#136185=EDGE_CURVE ( 'NONE', #71407, #64361, #48055, .T. ) ;
#136189=ORIENTED_EDGE ( 'NONE', *, *, #6927, .F. ) ;
#136190=VERTEX_POINT ( 'NONE', #5219 ) ;
#136191=EDGE_LOOP ( 'NONE', ( #62529, #92362, #97471, #103431 ) ) ;
#136193=DIRECTION ( 'NONE',  ( -0.7071067811865487940, 0.7071067811865463515, 0.000000000000000000 ) ) ;
#136194=CARTESIAN_POINT ( 'NONE',  ( -2.994519915287485734, 28.92564299267940342, 4.000000000000000000 ) ) ;
#136195=VECTOR ( 'NONE', #101389, 1000.000000000000000 ) ;
#136196=DIRECTION ( 'NONE',  ( 1.000000000000000000, 0.000000000000000000, 0.000000000000000000 ) ) ;
#136197=VERTEX_POINT ( 'NONE', #82830 ) ;
#136198=DIRECTION ( 'NONE',  ( -0.6830127018922180770, -0.6830127018922204085, -0.2588190451025213501 ) ) ;
#136199=VECTOR ( 'NONE', #135186, 1000.000000000000000 ) ;
#136200=DIRECTION ( 'NONE',  ( -0.7071067811865486830, 0.7071067811865464625, 0.000000000000000000 ) ) ;
#136201=EDGE_CURVE ( 'NONE', #116001, #52530, #27703, .T. ) ;
#136202=CARTESIAN_POINT ( 'NONE',  ( 8.292893218813400580, -9.740707523384184441, 5.000000000000000000 ) ) ;
#136203=LINE ( 'NONE', #94113, #102387 ) ;
#136204=VERTEX_POINT ( 'NONE', #58255 ) ;
#136206=ORIENTED_EDGE ( 'NONE', *, *, #25554, .F. ) ;
#136208=ORIENTED_EDGE ( 'NONE', *, *, #9795, .F. ) ;
#136209=EDGE_LOOP ( 'NONE', ( #14727, #21671, #86622, #56094 ) ) ;
#136210=EDGE_CURVE ( 'NONE', #70446, #18049, #103132, .T. ) ;
#136211=LINE ( 'NONE', #4940, #37779 ) ;
#136213=ORIENTED_EDGE ( 'NONE', *, *, #77225, .F. ) ;
#136214=CARTESIAN_POINT ( 'NONE',  ( -63.48921356237309510, -27.52281430457099631, 5.000000000000000000 ) ) ;
#136215=ORIENTED_EDGE ( 'NONE', *, *, #63185, .T. ) ;
#136216=LINE ( 'NONE', #36901, #96084 ) ;
#136217=LINE ( 'NONE', #47832, #46313 ) ;
#136219=PLANE ( 'NONE',  #48500 ) ;
#136220=CARTESIAN_POINT ( 'NONE',  ( -22.22850677138650610, 20.25929247661551003, 7.808871592221717783 ) ) ;
#136221=DIRECTION ( 'NONE',  ( 0.000000000000000000, 1.000000000000000000, 0.000000000000000000 ) ) ;
#136222=LINE ( 'NONE', #60861, #123286 ) ;
#136223=DIRECTION ( 'NONE',  ( 0.6830127018922180770, -0.6830127018922204085, -0.2588190451025213501 ) ) ;
#136227=CARTESIAN_POINT ( 'NONE',  ( 32.99999999999977263, 4.384688058510604058, -7.090945410444609465 ) ) ;
#136228=DIRECTION ( 'NONE',  ( -0.7071067811865486830, -0.7071067811865464625, 0.000000000000000000 ) ) ;
#136229=DIRECTION ( 'NONE',  ( -0.000000000000000000, 0.000000000000000000, 1.000000000000000000 ) ) ;
#136230=ORIENTED_EDGE ( 'NONE', *, *, #49602, .T. ) ;
#136231=ORIENTED_EDGE ( 'NONE', *, *, #45906, .T. ) ;
#136233=VERTEX_POINT ( 'NONE', #80685 ) ;
#136235=EDGE_CURVE ( 'NONE', #100840, #62352, #69828, .T. ) ;
#136236=CARTESIAN_POINT ( 'NONE',  ( 25.49999999999982947, -1.533600742197721134, 5.000000000000000000 ) ) ;
#136237=DIRECTION ( 'NONE',  ( 0.7071067811865487940, 0.7071067811865463515, -0.000000000000000000 ) ) ;
#136239=EDGE_LOOP ( 'NONE', ( #7654, #53554, #64347, #70539, #76396 ) ) ;
#136245=LINE ( 'NONE', #133417, #99592 ) ;
#136247=ADVANCED_FACE ( 'NONE', ( #37901 ), #102445, .T. ) ;
#136248=AXIS2_PLACEMENT_3D ( 'NONE', #98414, #120858, #65825 ) ;
#136249=EDGE_CURVE ( 'NONE', #66060, #12755, #135768, .T. ) ;
#136252=AXIS2_PLACEMENT_3D ( 'NONE', #53051, #133497, #34184 ) ;
#136253=LINE ( 'NONE', #112378, #121657 ) ;
#136254=CARTESIAN_POINT ( 'NONE',  ( 63.29974487139158867, -27.71228299555250274, 4.000000000000000000 ) ) ;
#136255=DIRECTION ( 'NONE',  ( 0.7071067811865486830, -0.7071067811865464625, -0.000000000000000000 ) ) ;
#136256=VECTOR ( 'NONE', #79388, 1000.000000000000000 ) ;
#136257=CARTESIAN_POINT ( 'NONE',  ( 30.18398860626900060, 28.73617430169808173, 5.000000000000000000 ) ) ;
#136259=ORIENTED_EDGE ( 'NONE', *, *, #13047, .F. ) ;
#136260=EDGE_LOOP ( 'NONE', ( #19003, #36370, #89944, #568 ) ) ;
#136262=ORIENTED_EDGE ( 'NONE', *, *, #37968, .F. ) ;
#136263=ADVANCED_FACE ( 'NONE', ( #2354 ), #25561, .F. ) ;
#136264=CARTESIAN_POINT ( 'NONE',  ( 20.70025512860841133, -27.71228299555191654, 4.000000000000000000 ) ) ;
#136265=VECTOR ( 'NONE', #74909, 1000.000000000000000 ) ;
#136266=PLANE ( 'NONE',  #22502 ) ;
#136269=CARTESIAN_POINT ( 'NONE',  ( 66.18398860626901126, 28.73617430169833753, 5.000000000000000000 ) ) ;
#136270=DIRECTION ( 'NONE',  ( -0.6830127018922181881, 0.6830127018922202975, -0.2588190451025214056 ) ) ;
#136271=VECTOR ( 'NONE', #4055, 999.9999999999998863 ) ;
#136274=ORIENTED_EDGE ( 'NONE', *, *, #51679, .T. ) ;
#136275=CARTESIAN_POINT ( 'NONE',  ( 8.206660635421465955, 21.75929247661549226, 4.998822639870702744 ) ) ;
#136276=CARTESIAN_POINT ( 'NONE',  ( 34.17183060077623225, 0.7592924766157086447, 4.000000000000000000 ) ) ;
#136277=VECTOR ( 'NONE', #64367, 1000.000000000000000 ) ;
#136278=ORIENTED_EDGE ( 'NONE', *, *, #11832, .F. ) ;
#136281=CARTESIAN_POINT ( 'NONE',  ( 10.49999999999992539, 11.52377502935403619, -1.522421517564110038 ) ) ;
#136287=CARTESIAN_POINT ( 'NONE',  ( -21.29974487139158512, -27.71228299555221142, 4.000000000000000000 ) ) ;
#136288=VERTEX_POINT ( 'NONE', #16841 ) ;
#136289=ORIENTED_EDGE ( 'NONE', *, *, #110385, .T. ) ;
#136291=DIRECTION ( 'NONE',  ( 0.7071067811865487940, 0.7071067811865463515, 0.000000000000000000 ) ) ;
#136292=VERTEX_POINT ( 'NONE', #115386 ) ;
#136293=VERTEX_POINT ( 'NONE', #114700 ) ;
#136294=VECTOR ( 'NONE', #13325, 1000.000000000000227 ) ;
#136295=EDGE_CURVE ( 'NONE', #45590, #102711, #60373, .T. ) ;
#136296=EDGE_CURVE ( 'NONE', #26486, #92120, #79996, .T. ) ;
#136297=DIRECTION ( 'NONE',  ( 0.6830127018922181881, 0.6830127018922202975, -0.2588190451025214056 ) ) ;
#136298=DIRECTION ( 'NONE',  ( 0.6830127018922181881, 0.6830127018922202975, -0.2588190451025214056 ) ) ;
#136299=ORIENTED_EDGE ( 'NONE', *, *, #134517, .F. ) ;
#136300=CARTESIAN_POINT ( 'NONE',  ( -21.48921356237309155, -27.52281430457070499, 5.000000000000000000 ) ) ;
#136301=PLANE ( 'NONE',  #10870 ) ;
#136302=CARTESIAN_POINT ( 'NONE',  ( 0.000000000000000000, 0.000000000000000000, 5.000000000000000000 ) ) ;
#136303=EDGE_CURVE ( 'NONE', #26845, #131176, #24854, .T. ) ;
#136304=CARTESIAN_POINT ( 'NONE',  ( -11.99999999999991296, -18.03360074219755660, 5.000000000000000000 ) ) ;
#136305=FACE_OUTER_BOUND ( 'NONE', #98411, .T. ) ;
#136306=FACE_BOUND ( 'NONE', #54182, .T. ) ;
#136307=ADVANCED_FACE ( 'NONE', ( #140738 ), #5921, .F. ) ;
#136309=CARTESIAN_POINT ( 'NONE',  ( -51.18398860626899705, 28.73617430169823095, 5.000000000000000000 ) ) ;
#136314=ORIENTED_EDGE ( 'NONE', *, *, #76083, .T. ) ;
#136316=ORIENTED_EDGE ( 'NONE', *, *, #16288, .F. ) ;
#136318=EDGE_CURVE ( 'NONE', #38121, #130029, #95097, .T. ) ;
#136320=EDGE_CURVE ( 'NONE', #95983, #88854, #139367, .T. ) ;
#136321=CARTESIAN_POINT ( 'NONE',  ( -30.29974487139158867, -27.71228299555227537, 4.000000000000000000 ) ) ;
#136323=CARTESIAN_POINT ( 'NONE',  ( -75.48921356237309510, -27.52281430457107803, 5.000000000000000000 ) ) ;
#136324=VERTEX_POINT ( 'NONE', #40054 ) ;
#136325=LINE ( 'NONE', #48616, #7418 ) ;
#136329=CARTESIAN_POINT ( 'NONE',  ( -34.42500000000001137, -6.022814304570508703, 5.000000000000000000 ) ) ;
#136330=CARTESIAN_POINT ( 'NONE',  ( 12.00548008471251293, 28.92564299267929684, 4.000000000000000000 ) ) ;
#136331=DIRECTION ( 'NONE',  ( 1.000000000000000000, 0.000000000000000000, 0.000000000000000000 ) ) ;
#136333=ORIENTED_EDGE ( 'NONE', *, *, #59981, .F. ) ;
#136334=EDGE_CURVE ( 'NONE', #110155, #39265, #118997, .T. ) ;
#136335=VERTEX_POINT ( 'NONE', #130621 ) ;
#136337=CARTESIAN_POINT ( 'NONE',  ( 5.999999999999958256, -13.97847968911259819, -0.1324546996126661491 ) ) ;
#136339=AXIS2_PLACEMENT_3D ( 'NONE', #63498, #75084, #98241 ) ;
#136340=ORIENTED_EDGE ( 'NONE', *, *, #126478, .T. ) ;
#136341=VECTOR ( 'NONE', #82142, 1000.000000000000000 ) ;
#136342=VECTOR ( 'NONE', #98513, 1000.000000000000000 ) ;
#136343=EDGE_LOOP ( 'NONE', ( #118099, #96540, #25973, #39198 ) ) ;
#136344=DIRECTION ( 'NONE',  ( 0.6830127018922180770, -0.6830127018922204085, -0.2588190451025213501 ) ) ;
#136346=EDGE_LOOP ( 'NONE', ( #10228, #73151, #101621, #19140 ) ) ;
#136347=EDGE_CURVE ( 'NONE', #49090, #55653, #28443, .T. ) ;
#136348=DIRECTION ( 'NONE',  ( 0.7071067811865487940, 0.7071067811865463515, -0.000000000000000000 ) ) ;
#136350=ORIENTED_EDGE ( 'NONE', *, *, #126773, .T. ) ;
#136352=EDGE_CURVE ( 'NONE', #62344, #112545, #120682, .T. ) ;
#136353=CARTESIAN_POINT ( 'NONE',  ( 4.499999999999976019, 7.466399257802187606, 5.000000000000000000 ) ) ;
#136354=VERTEX_POINT ( 'NONE', #50903 ) ;
#136356=DIRECTION ( 'NONE',  ( -0.7071067811865486830, 0.7071067811865464625, 0.000000000000000000 ) ) ;
#136357=DIRECTION ( 'NONE',  ( -0.7071067811865487940, 0.7071067811865463515, -0.000000000000000000 ) ) ;
#136358=ORIENTED_EDGE ( 'NONE', *, *, #53665, .F. ) ;
#136359=ORIENTED_EDGE ( 'NONE', *, *, #104908, .F. ) ;
#136362=AXIS2_PLACEMENT_3D ( 'NONE', #79757, #24595, #55833 ) ;
#136364=DIRECTION ( 'NONE',  ( -0.7071067811865486830, -0.7071067811865464625, 0.000000000000000000 ) ) ;
#136368=( BOUNDED_CURVE ( )  B_SPLINE_CURVE ( 3, ( #71938, #140038, #19659, #116110 ),
 .UNSPECIFIED., .F., .F. ) 
 B_SPLINE_CURVE_WITH_KNOTS ( ( 4, 4 ),
 ( 2.779374508378132713, 4.199602562396797190 ),
 .UNSPECIFIED. ) 
 CURVE ( )  GEOMETRIC_REPRESENTATION_ITEM ( )  RATIONAL_B_SPLINE_CURVE ( ( 1.000000000000000000, 0.8388583629366712646, 0.8388583629366712646, 1.000000000000000000 ) ) 
 REPRESENTATION_ITEM ( '' )  );
#136369=EDGE_LOOP ( 'NONE', ( #56908, #44260, #101155, #106394 ) ) ;
#136371=CARTESIAN_POINT ( 'NONE',  ( -16.49999999999988631, 22.01701374228154151, 2.453858888625669366 ) ) ;
#136373=CARTESIAN_POINT ( 'NONE',  ( -66.29974487139159578, -27.71228299555252406, 4.000000000000000000 ) ) ;
#136374=VECTOR ( 'NONE', #70696, 1000.000000000000000 ) ;
#136375=( BOUNDED_CURVE ( )  B_SPLINE_CURVE ( 3, ( #5011, #138432, #27500, #50008 ),
 .UNSPECIFIED., .F., .F. ) 
 B_SPLINE_CURVE_WITH_KNOTS ( ( 4, 4 ),
 ( 5.143245962375972091, 6.645403452391247079 ),
 .UNSPECIFIED. ) 
 CURVE ( )  GEOMETRIC_REPRESENTATION_ITEM ( )  RATIONAL_B_SPLINE_CURVE ( ( 1.000000000000000000, 0.8206354192515254997, 0.8206354192515254997, 1.000000000000000000 ) ) 
 REPRESENTATION_ITEM ( '' )  );
#136376=CARTESIAN_POINT ( 'NONE',  ( -75.18398860626899705, 28.73617430169839793, 5.000000000000000000 ) ) ;
#136377=VECTOR ( 'NONE', #80103, 1000.000000000000000 ) ;
#136378=ORIENTED_EDGE ( 'NONE', *, *, #116851, .F. ) ;
#136379=AXIS2_PLACEMENT_3D ( 'NONE', #141184, #43325, #7809 ) ;
#136380=CARTESIAN_POINT ( 'NONE',  ( 33.48921356237309510, -27.52281430457078670, 5.000000000000000000 ) ) ;
#136382=ORIENTED_EDGE ( 'NONE', *, *, #116768, .F. ) ;
#136384=VECTOR ( 'NONE', #99118, 1000.000000000000000 ) ;
#136386=ORIENTED_EDGE ( 'NONE', *, *, #42125, .F. ) ;
#136387=CARTESIAN_POINT ( 'NONE',  ( 41.99451991528749062, 28.92564299267967343, 4.000000000000000000 ) ) ;
#136388=PLANE ( 'NONE',  #102949 ) ;
#136389=CARTESIAN_POINT ( 'NONE',  ( -12.48921356237309155, -27.52281430457064104, 5.000000000000000000 ) ) ;
#136390=ORIENTED_EDGE ( 'NONE', *, *, #50851, .F. ) ;
#136391=FACE_OUTER_BOUND ( 'NONE', #31766, .T. ) ;
#136392=EDGE_CURVE ( 'NONE', #79017, #35337, #61795, .T. ) ;
#136393=CARTESIAN_POINT ( 'NONE',  ( 9.792893218813393474, -17.24070752338410628, 5.000000000000000000 ) ) ;
#136395=LINE ( 'NONE', #123421, #40202 ) ;
#136397=DIRECTION ( 'NONE',  ( -0.7071067811865486830, -0.7071067811865464625, 0.000000000000000000 ) ) ;
#136398=DIRECTION ( 'NONE',  ( -0.7071067811865486830, -0.7071067811865464625, 0.000000000000000000 ) ) ;
#136399=VERTEX_POINT ( 'NONE', #52311 ) ;
#136401=ORIENTED_EDGE ( 'NONE', *, *, #46140, .T. ) ;
#136403=ORIENTED_EDGE ( 'NONE', *, *, #53279, .F. ) ;
#136404=EDGE_LOOP ( 'NONE', ( #58910, #94389, #72024, #90488 ) ) ;
#136405=ORIENTED_EDGE ( 'NONE', *, *, #79733, .T. ) ;
#136406=CARTESIAN_POINT ( 'NONE',  ( -11.81601139373100651, 28.73617430169779041, 5.000000000000000000 ) ) ;
#136407=LINE ( 'NONE', #37098, #64769 ) ;
#136408=ORIENTED_EDGE ( 'NONE', *, *, #49823, .F. ) ;
#136409=CARTESIAN_POINT ( 'NONE',  ( -27.29974487139158512, -27.71228299555225405, 4.000000000000000000 ) ) ;
#136410=DIRECTION ( 'NONE',  ( -0.7071067811865486830, 0.7071067811865464625, 0.000000000000000000 ) ) ;
#136411=DIRECTION ( 'NONE',  ( 0.3543493200069162685, -0.000000000000000000, -0.9351131265310288487 ) ) ;
#136413=EDGE_CURVE ( 'NONE', #24882, #43020, #83546, .T. ) ;
#136414=ORIENTED_EDGE ( 'NONE', *, *, #40589, .F. ) ;
#136415=CARTESIAN_POINT ( 'NONE',  ( -17.99999999999986855, -19.22509904557638549, 1.855685503482138010 ) ) ;
#136416=FACE_OUTER_BOUND ( 'NONE', #96280, .T. ) ;
#136417=EDGE_CURVE ( 'NONE', #82894, #56980, #72704, .T. ) ;
#136418=CARTESIAN_POINT ( 'NONE',  ( -2.292893218813441880, -12.74070752338415602, 5.000000000000000000 ) ) ;
#136420=FACE_OUTER_BOUND ( 'NONE', #50365, .T. ) ;
#136421=DIRECTION ( 'NONE',  ( -0.7071067811865487940, 0.7071067811865463515, -0.000000000000000000 ) ) ;
#136422=CARTESIAN_POINT ( 'NONE',  ( -27.70710678118635428, 14.25929247661557397, 5.000000000000000000 ) ) ;
#136423=ADVANCED_FACE ( 'NONE', ( #117545 ), #18222, .F. ) ;
#136425=DIRECTION ( 'NONE',  ( 0.7071067811865486830, -0.7071067811865464625, -0.000000000000000000 ) ) ;
#136426=EDGE_LOOP ( 'NONE', ( #91071, #86461, #23813, #42996 ) ) ;
#136427=EDGE_LOOP ( 'NONE', ( #65319, #71778, #133440, #107136 ) ) ;
#136429=EDGE_LOOP ( 'NONE', ( #78444, #124111, #102786, #12288 ) ) ;
#136430=VERTEX_POINT ( 'NONE', #51624 ) ;
#136431=EDGE_CURVE ( 'NONE', #137039, #140166, #95817, .T. ) ;
#136433=VERTEX_POINT ( 'NONE', #129880 ) ;
#136434=PLANE ( 'NONE',  #124264 ) ;
#136435=CARTESIAN_POINT ( 'NONE',  ( -31.49999999999977973, 16.77039438581775954, 0.4657186855308451667 ) ) ;
#136436=EDGE_CURVE ( 'NONE', #86454, #2079, #84949, .T. ) ;
#136437=LINE ( 'NONE', #122894, #67400 ) ;
#136439=VERTEX_POINT ( 'NONE', #74818 ) ;
#136440=LINE ( 'NONE', #82116, #128922 ) ;
#136442=DIRECTION ( 'NONE',  ( 0.7071067811865487940, -0.7071067811865463515, 0.000000000000000000 ) ) ;
#136445=VECTOR ( 'NONE', #122842, 1000.000000000000000 ) ;
#136446=VECTOR ( 'NONE', #50350, 1000.000000000000227 ) ;
#136447=CARTESIAN_POINT ( 'NONE',  ( -28.49999999999981171, -4.216083040037277740, -7.486842126848595846 ) ) ;
#136450=CARTESIAN_POINT ( 'NONE',  ( 11.29289321881337926, 14.25929247661557753, 5.000000000000000000 ) ) ;
#136451=ORIENTED_EDGE ( 'NONE', *, *, #73143, .F. ) ;
#136452=VERTEX_POINT ( 'NONE', #55909 ) ;
#136453=PLANE ( 'NONE',  #130450 ) ;
#136454=DIRECTION ( 'NONE',  ( -0.6830127018922181881, 0.6830127018922202975, -0.2588190451025214056 ) ) ;
#136455=FACE_OUTER_BOUND ( 'NONE', #75859, .T. ) ;
#136456=EDGE_CURVE ( 'NONE', #87783, #123521, #100111, .T. ) ;
#136457=VECTOR ( 'NONE', #49951, 1000.000000000000000 ) ;
#136461=DIRECTION ( 'NONE',  ( 0.6830127018922181881, 0.6830127018922202975, -0.2588190451025214056 ) ) ;
#136462=ORIENTED_EDGE ( 'NONE', *, *, #111462, .F. ) ;
#136463=ORIENTED_EDGE ( 'NONE', *, *, #111940, .T. ) ;
#136465=VECTOR ( 'NONE', #88059, 1000.000000000000227 ) ;
#136466=CARTESIAN_POINT ( 'NONE',  ( -12.29974487139158512, -27.71228299555214747, 4.000000000000000000 ) ) ;
#136467=EDGE_LOOP ( 'NONE', ( #95960, #64640, #40616, #36874 ) ) ;
#136468=EDGE_CURVE ( 'NONE', #25060, #127256, #132036, .T. ) ;
#136469=EDGE_CURVE ( 'NONE', #16022, #11025, #45756, .T. ) ;
#136470=VECTOR ( 'NONE', #40018, 1000.000000000000000 ) ;
#136471=DIRECTION ( 'NONE',  ( 0.6830127018922180770, -0.6830127018922204085, -0.2588190451025213501 ) ) ;
#136472=ORIENTED_EDGE ( 'NONE', *, *, #41852, .T. ) ;
#136473=CARTESIAN_POINT ( 'NONE',  ( 3.328169399223493308, -18.74070752338410273, 4.000000000000000000 ) ) ;
#136474=AXIS2_PLACEMENT_3D ( 'NONE', #15361, #93685, #116131 ) ;
#136475=VECTOR ( 'NONE', #139312, 1000.000000000000227 ) ;
#136476=EDGE_CURVE ( 'NONE', #111687, #13822, #111695, .T. ) ;
#136477=LINE ( 'NONE', #58273, #55891 ) ;
#136478=AXIS2_PLACEMENT_3D ( 'NONE', #30119, #74369, #8338 ) ;
#136479=FACE_BOUND ( 'NONE', #89275, .T. ) ;
#136480=EDGE_CURVE ( 'NONE', #80319, #89805, #6761, .T. ) ;
#136481=DIRECTION ( 'NONE',  ( -0.7071067811865486830, 0.7071067811865464625, 0.000000000000000000 ) ) ;
#136483=CARTESIAN_POINT ( 'NONE',  ( 34.49999999999975842, 10.46425560840038571, 4.994342998332157890 ) ) ;
#136485=CARTESIAN_POINT ( 'NONE',  ( -11.51078643762690490, -27.52281430457047406, 5.000000000000000000 ) ) ;
#136486=ORIENTED_EDGE ( 'NONE', *, *, #20189, .T. ) ;
#136487=AXIS2_PLACEMENT_3D ( 'NONE', #1764, #100427, #34445 ) ;
#136488=PLANE ( 'NONE',  #41709 ) ;
#136490=VERTEX_POINT ( 'NONE', #56652 ) ;
#136492=ORIENTED_EDGE ( 'NONE', *, *, #132412, .T. ) ;
#136493=ADVANCED_FACE ( 'NONE', ( #54484 ), #12368, .F. ) ;
#136494=CARTESIAN_POINT ( 'NONE',  ( 29.99451991528749417, 28.92564299267958816, 4.000000000000000000 ) ) ;
#136495=CARTESIAN_POINT ( 'NONE',  ( 18.48921356237309510, -27.52281430457068367, 5.000000000000000000 ) ) ;
#136496=ORIENTED_EDGE ( 'NONE', *, *, #143015, .F. ) ;
#136497=AXIS2_PLACEMENT_3D ( 'NONE', #109124, #60115, #31582 ) ;
#136498=ADVANCED_FACE ( 'NONE', ( #1469 ), #108802, .F. ) ;
#136500=PLANE ( 'NONE',  #106080 ) ;
#136502=FACE_OUTER_BOUND ( 'NONE', #130878, .T. ) ;
#136503=DIRECTION ( 'NONE',  ( 0.7071067811865486830, -0.7071067811865464625, -0.000000000000000000 ) ) ;
#136506=CARTESIAN_POINT ( 'NONE',  ( 14.39158342593605155, -0.5643469832421100785, 4.274152510792124104 ) ) ;
#136507=DIRECTION ( 'NONE',  ( -0.000000000000000000, 0.000000000000000000, 1.000000000000000000 ) ) ;
#136508=ORIENTED_EDGE ( 'NONE', *, *, #44245, .F. ) ;
#136510=ORIENTED_EDGE ( 'NONE', *, *, #101966, .T. ) ;
#136511=DIRECTION ( 'NONE',  ( -0.7071067811865486830, -0.7071067811865464625, 0.000000000000000000 ) ) ;
#136512=CARTESIAN_POINT ( 'NONE',  ( 33.18398860626899705, 28.73617430169810305, 5.000000000000000000 ) ) ;
#136513=ORIENTED_EDGE ( 'NONE', *, *, #65488, .F. ) ;
#136514=CARTESIAN_POINT ( 'NONE',  ( -33.79289321881321939, -20.24070752338407431, 5.000000000000000000 ) ) ;
#136515=EDGE_CURVE ( 'NONE', #56258, #63020, #142896, .T. ) ;
#136516=LINE ( 'NONE', #126359, #111818 ) ;
#136518=LINE ( 'NONE', #92294, #7873 ) ;
#136519=ORIENTED_EDGE ( 'NONE', *, *, #16107, .F. ) ;
#136520=DIRECTION ( 'NONE',  ( -0.6830127018922181881, 0.6830127018922202975, -0.2588190451025214056 ) ) ;
#136521=CARTESIAN_POINT ( 'NONE',  ( -17.20829011259837671, -2.505970753447624766, 4.303104124266146080 ) ) ;
#136522=CARTESIAN_POINT ( 'NONE',  ( 24.29974487139158867, -27.71228299555223273, 4.000000000000000000 ) ) ;
#136523=DIRECTION ( 'NONE',  ( 0.000000000000000000, 1.000000000000000000, 0.000000000000000000 ) ) ;
#136524=VERTEX_POINT ( 'NONE', #43578 ) ;
#136525=ORIENTED_EDGE ( 'NONE', *, *, #70857, .T. ) ;
#136526=DIRECTION ( 'NONE',  ( 1.000000000000000000, -0.000000000000000000, 0.000000000000000000 ) ) ;
#136527=DIRECTION ( 'NONE',  ( -0.000000000000000000, 0.000000000000000000, 1.000000000000000000 ) ) ;
#136528=DIRECTION ( 'NONE',  ( 0.7071067811865486830, -0.7071067811865464625, -0.000000000000000000 ) ) ;
#136530=CARTESIAN_POINT ( 'NONE',  ( 33.18398860626899705, 28.73617430169810305, 5.000000000000000000 ) ) ;
#136531=CARTESIAN_POINT ( 'NONE',  ( -21.48921356237309155, -27.52281430457070499, 5.000000000000000000 ) ) ;
#136532=CARTESIAN_POINT ( 'NONE',  ( 29.99999999999979039, -21.03360074219752462, 5.000000000000000000 ) ) ;
#136533=FACE_OUTER_BOUND ( 'NONE', #34330, .T. ) ;
#136534=CARTESIAN_POINT ( 'NONE',  ( 69.48921356237309510, -27.52281430457103895, 5.000000000000000000 ) ) ;
#136535=VECTOR ( 'NONE', #12554, 1000.000000000000000 ) ;
#136536=EDGE_LOOP ( 'NONE', ( #39299, #83992, #3687, #77206 ) ) ;
#136537=AXIS2_PLACEMENT_3D ( 'NONE', #82, #56702, #24030 ) ;
#136538=VECTOR ( 'NONE', #101243, 1000.000000000000000 ) ;
#136540=CARTESIAN_POINT ( 'NONE',  ( -4.410090645198292414, 9.759292476615618384, 11.28811694763777851 ) ) ;
#136541=DIRECTION ( 'NONE',  ( -0.000000000000000000, 1.000000000000000000, -0.000000000000000000 ) ) ;
#136542=CARTESIAN_POINT ( 'NONE',  ( 8.999999999999944933, -3.412538124160723108, 4.000000000000000000 ) ) ;
#136544=LINE ( 'NONE', #23508, #47436 ) ;
#136545=LINE ( 'NONE', #38680, #101626 ) ;
#136546=ORIENTED_EDGE ( 'NONE', *, *, #72059, .F. ) ;
#136547=VERTEX_POINT ( 'NONE', #53767 ) ;
#136548=CARTESIAN_POINT ( 'NONE',  ( 9.183988606268997046, 28.73617430169793607, 5.000000000000000000 ) ) ;
#136549=AXIS2_PLACEMENT_3D ( 'NONE', #58560, #36738, #80978 ) ;
#136551=LINE ( 'NONE', #47470, #20463 ) ;
#136552=VECTOR ( 'NONE', #4923, 1000.000000000000114 ) ;
#136554=DIRECTION ( 'NONE',  ( -0.7071067811865487940, 0.7071067811865463515, 0.000000000000000000 ) ) ;
#136555=CARTESIAN_POINT ( 'NONE',  ( 14.81601139373099585, 28.73617430169776910, 5.000000000000000000 ) ) ;
#136556=ORIENTED_EDGE ( 'NONE', *, *, #39137, .T. ) ;
#136558=EDGE_CURVE ( 'NONE', #118125, #100624, #87795, .T. ) ;
#136559=DIRECTION ( 'NONE',  ( -0.7071067811865486830, -0.7071067811865464625, 0.000000000000000000 ) ) ;
#136560=VECTOR ( 'NONE', #56765, 1000.000000000000000 ) ;
#136564=VECTOR ( 'NONE', #75837, 1000.000000000000227 ) ;
#136566=FACE_OUTER_BOUND ( 'NONE', #835, .T. ) ;
#136567=VERTEX_POINT ( 'NONE', #142206 ) ;
#136568=CARTESIAN_POINT ( 'NONE',  ( 19.49999999999986144, -20.53675388469228835, 2.352720554255939511 ) ) ;
#136569=ADVANCED_FACE ( 'NONE', ( #42895 ), #89234, .F. ) ;
#136570=ORIENTED_EDGE ( 'NONE', *, *, #90195, .F. ) ;
#136571=CARTESIAN_POINT ( 'NONE',  ( 14.99999999999989875, -4.068876922607767455, 4.000000000000000000 ) ) ;
#136572=VECTOR ( 'NONE', #91348, 1000.000000000000000 ) ;
#136573=CARTESIAN_POINT ( 'NONE',  ( 23.99451991528749062, 28.92564299267954908, 4.000000000000000000 ) ) ;
#136574=CARTESIAN_POINT ( 'NONE',  ( -5.207106781186511490, 18.75929247661552779, 5.000000000000000000 ) ) ;
#136575=EDGE_CURVE ( 'NONE', #97535, #89442, #21830, .T. ) ;
#136576=CARTESIAN_POINT ( 'NONE',  ( -14.51078643762690490, -27.52281430457045275, 5.000000000000000000 ) ) ;
#136577=DIRECTION ( 'NONE',  ( -0.7071067811865486830, -0.7071067811865464625, 0.000000000000000000 ) ) ;
#136579=EDGE_CURVE ( 'NONE', #73550, #30286, #65368, .T. ) ;
#136580=EDGE_CURVE ( 'NONE', #56496, #113570, #10918, .T. ) ;
#136581=AXIS2_PLACEMENT_3D ( 'NONE', #57377, #67544, #55219 ) ;
#136582=ORIENTED_EDGE ( 'NONE', *, *, #93868, .F. ) ;
#136583=CARTESIAN_POINT ( 'NONE',  ( 26.81601139373100651, 28.73617430169768738, 5.000000000000000000 ) ) ;
#136585=VECTOR ( 'NONE', #14304, 1000.000000000000000 ) ;
#136586=FACE_OUTER_BOUND ( 'NONE', #113305, .T. ) ;
#136587=CARTESIAN_POINT ( 'NONE',  ( -48.29974487139158867, -27.71228299555239971, 4.000000000000000000 ) ) ;
#136588=EDGE_CURVE ( 'NONE', #95640, #111746, #25, .T. ) ;
#136590=ADVANCED_FACE ( 'NONE', ( #33460 ), #22507, .T. ) ;
#136591=DIRECTION ( 'NONE',  ( -0.7071067811865486830, -0.7071067811865464625, -0.000000000000000000 ) ) ;
#136592=VECTOR ( 'NONE', #98855, 1000.000000000000000 ) ;
#136593=ORIENTED_EDGE ( 'NONE', *, *, #2735, .T. ) ;
#136596=CARTESIAN_POINT ( 'NONE',  ( 0.000000000000000000, 0.000000000000000000, 5.000000000000000000 ) ) ;
#136597=ADVANCED_FACE ( 'NONE', ( #36284 ), #93511, .F. ) ;
#136598=CARTESIAN_POINT ( 'NONE',  ( -34.92500000000001137, 22.22500000000000142, 4.000000000000000000 ) ) ;
#136600=VECTOR ( 'NONE', #106066, 1000.000000000000227 ) ;
#136602=CARTESIAN_POINT ( 'NONE',  ( -13.00193056682089043, -22.22500000000000142, 4.500000000000000888 ) ) ;
#136603=EDGE_CURVE ( 'NONE', #49880, #111254, #113105, .T. ) ;
#136604=LINE ( 'NONE', #126439, #44349 ) ;
#136607=VERTEX_POINT ( 'NONE', #92066 ) ;
#136609=VECTOR ( 'NONE', #54538, 1000.000000000000000 ) ;
#136612=CARTESIAN_POINT ( 'NONE',  ( 0.000000000000000000, 0.000000000000000000, 5.000000000000000000 ) ) ;
#136614=PLANE ( 'NONE',  #141450 ) ;
#136615=DIRECTION ( 'NONE',  ( -0.7071067811865486830, -0.7071067811865464625, 0.000000000000000000 ) ) ;
#136616=ORIENTED_EDGE ( 'NONE', *, *, #91906, .T. ) ;
#136617=LINE ( 'NONE', #72135, #73886 ) ;
#136618=CARTESIAN_POINT ( 'NONE',  ( 16.49999999999988276, -16.91253812416058722, 4.000000000000000000 ) ) ;
#136619=DIRECTION ( 'NONE',  ( 0.7071067811865486830, -0.7071067811865464625, -0.000000000000000000 ) ) ;
#136620=EDGE_CURVE ( 'NONE', #84665, #11791, #102969, .T. ) ;
#136621=VECTOR ( 'NONE', #71522, 1000.000000000000000 ) ;
#136622=CARTESIAN_POINT ( 'NONE',  ( -22.49999999999983302, -5.947814304570768762, 5.000000000000000000 ) ) ;
#136623=VECTOR ( 'NONE', #102342, 1000.000000000000227 ) ;
#136624=ORIENTED_EDGE ( 'NONE', *, *, #9920, .F. ) ;
#136625=ORIENTED_EDGE ( 'NONE', *, *, #8312, .F. ) ;
#136627=DIRECTION ( 'NONE',  ( 0.3543493200069162685, -0.000000000000000000, -0.9351131265310288487 ) ) ;
#136628=CARTESIAN_POINT ( 'NONE',  ( -34.49999999999976552, -4.796895815301057908, -3.611700055028757461 ) ) ;
#136630=FACE_OUTER_BOUND ( 'NONE', #13402, .T. ) ;
#136632=ORIENTED_EDGE ( 'NONE', *, *, #137614, .F. ) ;
#136633=ORIENTED_EDGE ( 'NONE', *, *, #52022, .F. ) ;
#136634=DIRECTION ( 'NONE',  ( -0.000000000000000000, 0.000000000000000000, 1.000000000000000000 ) ) ;
#136635=PLANE ( 'NONE',  #9769 ) ;
#136636=ADVANCED_FACE ( 'NONE', ( #123308 ), #124007, .F. ) ;
#136637=VECTOR ( 'NONE', #70946, 999.9999999999998863 ) ;
#136640=ORIENTED_EDGE ( 'NONE', *, *, #91099, .T. ) ;
#136641=EDGE_CURVE ( 'NONE', #3062, #66852, #21643, .T. ) ;
#136643=DIRECTION ( 'NONE',  ( 0.7071067811865487940, 0.7071067811865463515, 0.000000000000000000 ) ) ;
#136645=VECTOR ( 'NONE', #90768, 1000.000000000000000 ) ;
#136646=VECTOR ( 'NONE', #35504, 999.9999999999998863 ) ;
#136647=EDGE_CURVE ( 'NONE', #9288, #10232, #81961, .T. ) ;
#136648=AXIS2_PLACEMENT_3D ( 'NONE', #17912, #95500, #96899 ) ;
#136649=FACE_BOUND ( 'NONE', #75684, .T. ) ;
#136650=PLANE ( 'NONE',  #22369 ) ;
#136651=CARTESIAN_POINT ( 'NONE',  ( 3.717577386425651387, -21.73023691814492153, 5.000000000000000000 ) ) ;
#136652=LINE ( 'NONE', #74829, #20430 ) ;
#136653=VECTOR ( 'NONE', #4238, 1000.000000000000227 ) ;
#136654=CARTESIAN_POINT ( 'NONE',  ( -45.48921356237309510, -27.52281430457087197, 5.000000000000000000 ) ) ;
#136656=DIRECTION ( 'NONE',  ( 0.7071067811865487940, 0.7071067811865463515, -0.000000000000000000 ) ) ;
#136658=ORIENTED_EDGE ( 'NONE', *, *, #19049, .T. ) ;
#136659=ORIENTED_EDGE ( 'NONE', *, *, #86915, .T. ) ;
#136661=ORIENTED_EDGE ( 'NONE', *, *, #69180, .F. ) ;
#136662=EDGE_CURVE ( 'NONE', #137138, #77634, #48579, .T. ) ;
#136664=VECTOR ( 'NONE', #31733, 1000.000000000000000 ) ;
#136665=PLANE ( 'NONE',  #9921 ) ;
#136667=CARTESIAN_POINT ( 'NONE',  ( 15.18398860626900237, 28.73617430169797871, 5.000000000000000000 ) ) ;
#136668=ORIENTED_EDGE ( 'NONE', *, *, #16040, .T. ) ;
#136670=AXIS2_PLACEMENT_3D ( 'NONE', #43606, #77686, #109577 ) ;
#136671=DIRECTION ( 'NONE',  ( 1.000000000000000000, 0.000000000000000000, 0.000000000000000000 ) ) ;
#136672=DIRECTION ( 'NONE',  ( -0.000000000000000000, 0.3543493200069153248, 0.9351131265310292928 ) ) ;
#136673=CARTESIAN_POINT ( 'NONE',  ( -3.005480084712505828, 28.92564299267936079, 4.000000000000000000 ) ) ;
#136674=DIRECTION ( 'NONE',  ( 0.7071067811865487940, 0.7071067811865463515, 0.000000000000000000 ) ) ;
#136675=VECTOR ( 'NONE', #120710, 1000.000000000000000 ) ;
#136676=CARTESIAN_POINT ( 'NONE',  ( -34.49999999999976552, 3.653845994658358354, -4.504631822206292213 ) ) ;
#136678=ORIENTED_EDGE ( 'NONE', *, *, #121287, .T. ) ;
#136679=CIRCLE ( 'NONE', #74194, 5.968999999999998529 ) ;
#136680=FACE_OUTER_BOUND ( 'NONE', #123123, .T. ) ;
#136681=DIRECTION ( 'NONE',  ( -0.7071067811865487940, 0.7071067811865463515, 0.000000000000000000 ) ) ;
#136682=ORIENTED_EDGE ( 'NONE', *, *, #67435, .T. ) ;
#136683=EDGE_CURVE ( 'NONE', #12215, #114108, #13069, .T. ) ;
#136688=ORIENTED_EDGE ( 'NONE', *, *, #599, .T. ) ;
#136689=VECTOR ( 'NONE', #124279, 1000.000000000000000 ) ;
#136692=ORIENTED_EDGE ( 'NONE', *, *, #74796, .T. ) ;
#136693=DIRECTION ( 'NONE',  ( -0.7071067811865486830, -0.7071067811865464625, 0.000000000000000000 ) ) ;
#136694=VERTEX_POINT ( 'NONE', #47898 ) ;
#136696=DIRECTION ( 'NONE',  ( -0.6830127018922181881, 0.6830127018922202975, -0.2588190451025214056 ) ) ;
#136697=CARTESIAN_POINT ( 'NONE',  ( 44.99451991528749772, 28.92564299267969474, 4.000000000000000000 ) ) ;
#136699=ORIENTED_EDGE ( 'NONE', *, *, #138991, .F. ) ;
#136700=EDGE_CURVE ( 'NONE', #137194, #871, #24673, .T. ) ;
#136702=LINE ( 'NONE', #37406, #20579 ) ;
#136703=EDGE_LOOP ( 'NONE', ( #65555, #107113, #140558, #10945 ) ) ;
#136704=EDGE_CURVE ( 'NONE', #80143, #139533, #4282, .T. ) ;
#136705=DIRECTION ( 'NONE',  ( -0.7071067811865486830, 0.7071067811865464625, 0.000000000000000000 ) ) ;
#136706=ORIENTED_EDGE ( 'NONE', *, *, #96818, .F. ) ;
#136707=ORIENTED_EDGE ( 'NONE', *, *, #13906, .F. ) ;
#136709=VERTEX_POINT ( 'NONE', #68932 ) ;
#136710=DIRECTION ( 'NONE',  ( 0.3543493200069162685, -0.000000000000000000, -0.9351131265310288487 ) ) ;
#136713=CARTESIAN_POINT ( 'NONE',  ( -7.033400323430184287, 6.759292476615645917, 12.28218704918520565 ) ) ;
#136714=DIRECTION ( 'NONE',  ( -0.7071067811865486830, -0.7071067811865464625, 0.000000000000000000 ) ) ;
#136715=ADVANCED_FACE ( 'NONE', ( #60185 ), #3606, .F. ) ;
#136716=LINE ( 'NONE', #101237, #120540 ) ;
#136717=ORIENTED_EDGE ( 'NONE', *, *, #98226, .T. ) ;
#136718=AXIS2_PLACEMENT_3D ( 'NONE', #138027, #61912, #135881 ) ;
#136719=CARTESIAN_POINT ( 'NONE',  ( 0.000000000000000000, 0.000000000000000000, 5.000000000000000000 ) ) ;
#136721=DIRECTION ( 'NONE',  ( 0.7071067811865486830, -0.7071067811865464625, -0.000000000000000000 ) ) ;
#136724=EDGE_LOOP ( 'NONE', ( #30332, #107912, #127646, #68241 ) ) ;
#136725=ORIENTED_EDGE ( 'NONE', *, *, #77518, .F. ) ;
#136726=ORIENTED_EDGE ( 'NONE', *, *, #112682, .F. ) ;
#136728=DIRECTION ( 'NONE',  ( -0.7071067811865486830, -0.7071067811865464625, -0.000000000000000000 ) ) ;
#136729=FACE_OUTER_BOUND ( 'NONE', #110085, .T. ) ;
#136732=CARTESIAN_POINT ( 'NONE',  ( -6.183988606268994381, 28.73617430169791476, 5.000000000000000000 ) ) ;
#136734=LINE ( 'NONE', #37451, #39542 ) ;
#136735=AXIS2_PLACEMENT_3D ( 'NONE', #53948, #62665, #18395 ) ;
#136736=CARTESIAN_POINT ( 'NONE',  ( 29.67183060077626422, -12.74070752338415247, 4.000000000000000000 ) ) ;
#136737=CARTESIAN_POINT ( 'NONE',  ( 32.99999999999977973, 2.966399257802230682, 5.000000000000000000 ) ) ;
#136738=CARTESIAN_POINT ( 'NONE',  ( 12.78162688292485782, 21.74787736706806385, 4.999607392498048419 ) ) ;
#136739=DIRECTION ( 'NONE',  ( 0.000000000000000000, 1.000000000000000000, 0.000000000000000000 ) ) ;
#136740=VERTEX_POINT ( 'NONE', #91393 ) ;
#136741=VECTOR ( 'NONE', #100196, 1000.000000000000000 ) ;
#136742=VECTOR ( 'NONE', #74534, 1000.000000000000227 ) ;
#136743=AXIS2_PLACEMENT_3D ( 'NONE', #109820, #106384, #51352 ) ;
#136744=DIRECTION ( 'NONE',  ( 0.6830127018922181881, 0.6830127018922202975, -0.2588190451025214056 ) ) ;
#136745=ORIENTED_EDGE ( 'NONE', *, *, #110942, .F. ) ;
#136746=VECTOR ( 'NONE', #109055, 1000.000000000000227 ) ;
#136747=LINE ( 'NONE', #125899, #85346 ) ;
#136748=DIRECTION ( 'NONE',  ( -0.3543493200069162685, -0.000000000000000000, -0.9351131265310288487 ) ) ;
#136749=VERTEX_POINT ( 'NONE', #36974 ) ;
#136750=CARTESIAN_POINT ( 'NONE',  ( 34.17183060077623225, 9.759292476615620160, 4.000000000000000000 ) ) ;
#136751=FACE_OUTER_BOUND ( 'NONE', #34281, .T. ) ;
#136752=EDGE_CURVE ( 'NONE', #138807, #14297, #137016, .T. ) ;
#136753=EDGE_LOOP ( 'NONE', ( #52256, #88430, #45561 ) ) ;
#136754=LINE ( 'NONE', #36050, #134109 ) ;
#136755=ORIENTED_EDGE ( 'NONE', *, *, #119227, .T. ) ;
#136756=VECTOR ( 'NONE', #137522, 1000.000000000000227 ) ;
#136758=CARTESIAN_POINT ( 'NONE',  ( -62.99451991528749772, 28.92564299267982264, 4.000000000000000000 ) ) ;
#136759=EDGE_CURVE ( 'NONE', #81264, #7112, #37721, .T. ) ;
#136760=EDGE_CURVE ( 'NONE', #60766, #127270, #71069, .T. ) ;
#136762=EDGE_CURVE ( 'NONE', #70580, #55207, #71777, .T. ) ;
#136763=DIRECTION ( 'NONE',  ( 1.000000000000000000, 0.000000000000000000, 0.000000000000000000 ) ) ;
#136766=EDGE_CURVE ( 'NONE', #20476, #83916, #78365, .T. ) ;
#136767=VECTOR ( 'NONE', #88544, 1000.000000000000000 ) ;
#136769=DIRECTION ( 'NONE',  ( 0.3543493200069162685, -0.000000000000000000, -0.9351131265310288487 ) ) ;
#136770=EDGE_CURVE ( 'NONE', #104374, #16647, #7171, .T. ) ;
#136771=DIRECTION ( 'NONE',  ( 0.3543493200069162685, -0.000000000000000000, -0.9351131265310288487 ) ) ;
#136773=CARTESIAN_POINT ( 'NONE',  ( -15.21590231913187452, -1.409216073889146381, 4.328383627671533063 ) ) ;
#136775=LINE ( 'NONE', #70838, #90663 ) ;
#136776=ADVANCED_FACE ( 'NONE', ( #73901 ), #107915, .F. ) ;
#136777=VERTEX_POINT ( 'NONE', #28972 ) ;
#136778=AXIS2_PLACEMENT_3D ( 'NONE', #20570, #62686, #38248 ) ;
#136779=DIRECTION ( 'NONE',  ( -0.6830127018922181881, 0.6830127018922202975, -0.2588190451025214056 ) ) ;
#136781=EDGE_LOOP ( 'NONE', ( #24222, #84482, #139254, #101969 ) ) ;
#136782=VECTOR ( 'NONE', #62650, 1000.000000000000000 ) ;
#136784=VECTOR ( 'NONE', #68359, 999.9999999999998863 ) ;
#136785=CARTESIAN_POINT ( 'NONE',  ( 5.510786437626906675, -27.52281430457051314, 5.000000000000000000 ) ) ;
#136786=PLANE ( 'NONE',  #94741 ) ;
#136787=CARTESIAN_POINT ( 'NONE',  ( -20.99999999999985079, 16.55218569542900298, 5.000000000000000000 ) ) ;
#136788=CARTESIAN_POINT ( 'NONE',  ( -33.18398860626899705, 28.73617430169810305, 5.000000000000000000 ) ) ;
#136789=ORIENTED_EDGE ( 'NONE', *, *, #2054, .T. ) ;
#136792=EDGE_CURVE ( 'NONE', #48205, #111455, #40575, .T. ) ;
#136793=CARTESIAN_POINT ( 'NONE',  ( 5.999999999999967137, 4.931123077392134846, 4.000000000000000000 ) ) ;
#136794=VERTEX_POINT ( 'NONE', #96320 ) ;
#136795=CARTESIAN_POINT ( 'NONE',  ( 4.171830600776437414, -20.24070752338407431, 4.000000000000000000 ) ) ;
#136797=LINE ( 'NONE', #112903, #59089 ) ;
#136798=VERTEX_POINT ( 'NONE', #127567 ) ;
#136799=CARTESIAN_POINT ( 'NONE',  ( -48.29974487139158867, -27.71228299555239971, 4.000000000000000000 ) ) ;
#136800=CARTESIAN_POINT ( 'NONE',  ( -20.29298673570681544, -21.74070752338406720, 4.999753212805217117 ) ) ;
#136801=CARTESIAN_POINT ( 'NONE',  ( -22.49999999999984013, -7.912538124160678699, 4.000000000000000000 ) ) ;
#136802=EDGE_CURVE ( 'NONE', #68809, #17816, #39872, .T. ) ;
#136805=EDGE_LOOP ( 'NONE', ( #45810, #110573, #135954 ) ) ;
#136806=ORIENTED_EDGE ( 'NONE', *, *, #20544, .T. ) ;
#136808=VECTOR ( 'NONE', #81783, 1000.000000000000227 ) ;
#136809=ORIENTED_EDGE ( 'NONE', *, *, #32197, .F. ) ;
#136810=PLANE ( 'NONE',  #98379 ) ;
#136811=LINE ( 'NONE', #126630, #138280 ) ;
#136813=DIRECTION ( 'NONE',  ( -0.000000000000000000, 0.3543493200069153248, 0.9351131265310292928 ) ) ;
#136815=ORIENTED_EDGE ( 'NONE', *, *, #129966, .T. ) ;
#136817=LINE ( 'NONE', #37528, #53679 ) ;
#136819=EDGE_LOOP ( 'NONE', ( #113324, #95761, #32850, #74093 ) ) ;
#136820=LINE ( 'NONE', #136106, #30401 ) ;
#136821=EDGE_CURVE ( 'NONE', #28133, #64959, #5756, .T. ) ;
#136823=CARTESIAN_POINT ( 'NONE',  ( 0.000000000000000000, 0.000000000000000000, 5.000000000000000000 ) ) ;
#136824=VECTOR ( 'NONE', #125130, 1000.000000000000000 ) ;
#136825=VERTEX_POINT ( 'NONE', #94209 ) ;
#136826=ORIENTED_EDGE ( 'NONE', *, *, #121931, .F. ) ;
#136827=PLANE ( 'NONE',  #83999 ) ;
#136828=LINE ( 'NONE', #126650, #105674 ) ;
#136829=CARTESIAN_POINT ( 'NONE',  ( 11.99999999999990230, 2.587461875839226710, 4.000000000000000000 ) ) ;
#136831=LINE ( 'NONE', #60008, #27074 ) ;
#136832=ADVANCED_FACE ( 'NONE', ( #128293 ), #61626, .F. ) ;
#136833=CARTESIAN_POINT ( 'NONE',  ( 36.18398860626899705, 28.73617430169812437, 5.000000000000000000 ) ) ;
#136834=CARTESIAN_POINT ( 'NONE',  ( -5.999999999999954703, 1.552185695429154633, 5.000000000000000000 ) ) ;
#136835=EDGE_LOOP ( 'NONE', ( #90661, #121589, #11347, #108510, #83576 ) ) ;
#136838=EDGE_CURVE ( 'NONE', #101323, #24388, #107228, .T. ) ;
#136839=ORIENTED_EDGE ( 'NONE', *, *, #69966, .T. ) ;
#136840=VECTOR ( 'NONE', #29722, 1000.000000000000000 ) ;
#136841=VECTOR ( 'NONE', #15369, 1000.000000000000000 ) ;
#136842=DIRECTION ( 'NONE',  ( -0.000000000000000000, 0.3543493200069153248, 0.9351131265310292928 ) ) ;
#136843=EDGE_LOOP ( 'NONE', ( #138571, #89723, #1273, #119935 ) ) ;
#136845=DIRECTION ( 'NONE',  ( 0.6830127018922180770, -0.6830127018922204085, -0.2588190451025213501 ) ) ;
#136846=EDGE_CURVE ( 'NONE', #110710, #40937, #118820, .T. ) ;
#136847=CARTESIAN_POINT ( 'NONE',  ( -0.7928932188134494297, 9.759292476615621936, 5.000000000000000000 ) ) ;
#136850=VECTOR ( 'NONE', #141388, 1000.000000000000000 ) ;
#136851=VECTOR ( 'NONE', #64421, 1000.000000000000000 ) ;
#136852=LINE ( 'NONE', #92616, #88473 ) ;
#136854=VECTOR ( 'NONE', #75576, 1000.000000000000000 ) ;
#136855=CARTESIAN_POINT ( 'NONE',  ( 33.75860074219772855, 21.72500000000000142, 5.000000000000000000 ) ) ;
#136857=ORIENTED_EDGE ( 'NONE', *, *, #125911, .T. ) ;
#136858=LINE ( 'NONE', #81803, #8808 ) ;
#136859=ADVANCED_FACE ( 'NONE', ( #6441 ), #72520, .F. ) ;
#136860=ORIENTED_EDGE ( 'NONE', *, *, #77564, .T. ) ;
#136861=ORIENTED_EDGE ( 'NONE', *, *, #114842, .F. ) ;
#136862=CARTESIAN_POINT ( 'NONE',  ( -27.18398860626900060, 28.73617430169806042, 5.000000000000000000 ) ) ;
#136863=ORIENTED_EDGE ( 'NONE', *, *, #81199, .T. ) ;
#136864=EDGE_LOOP ( 'NONE', ( #107883, #47813, #82178 ) ) ;
#136865=VECTOR ( 'NONE', #40889, 1000.000000000000000 ) ;
#136867=VERTEX_POINT ( 'NONE', #28261 ) ;
#136868=LINE ( 'NONE', #103503, #46610 ) ;
#136869=ADVANCED_FACE ( 'NONE', ( #84774 ), #94912, .F. ) ;
#136870=DIRECTION ( 'NONE',  ( 0.6830127018922181881, 0.6830127018922202975, -0.2588190451025214056 ) ) ;
#136872=CARTESIAN_POINT ( 'NONE',  ( 34.92499999999998295, -22.22500000000000142, 4.500000000000000888 ) ) ;
#136873=VECTOR ( 'NONE', #60940, 1000.000000000000000 ) ;
#136874=CARTESIAN_POINT ( 'NONE',  ( -34.92500000000001137, 0.8561230773924295434, 4.000000000000000000 ) ) ;
#136875=LINE ( 'NONE', #37582, #66466 ) ;
#136881=VECTOR ( 'NONE', #1651, 1000.000000000000227 ) ;
#136882=DIRECTION ( 'NONE',  ( 0.3543493200069162685, -0.000000000000000000, -0.9351131265310288487 ) ) ;
#136883=ORIENTED_EDGE ( 'NONE', *, *, #33995, .T. ) ;
#136884=VECTOR ( 'NONE', #15706, 1000.000000000000000 ) ;
#136885=ADVANCED_FACE ( 'NONE', ( #82642 ), #89078, .T. ) ;
#136887=DIRECTION ( 'NONE',  ( 0.7071067811865487940, -0.7071067811865463515, 0.000000000000000000 ) ) ;
#136888=ORIENTED_EDGE ( 'NONE', *, *, #20544, .F. ) ;
#136889=VECTOR ( 'NONE', #70242, 1000.000000000000000 ) ;
#136890=EDGE_LOOP ( 'NONE', ( #31936, #10984, #88623, #125658 ) ) ;
#136891=LINE ( 'NONE', #13654, #37897 ) ;
#136892=ORIENTED_EDGE ( 'NONE', *, *, #70977, .F. ) ;
#136893=DIRECTION ( 'NONE',  ( 0.6830127018922181881, 0.6830127018922202975, -0.2588190451025214056 ) ) ;
#136894=CARTESIAN_POINT ( 'NONE',  ( 0.000000000000000000, 0.000000000000000000, 5.000000000000000000 ) ) ;
#136895=AXIS2_PLACEMENT_3D ( 'NONE', #79034, #55840, #100046 ) ;
#136897=EDGE_CURVE ( 'NONE', #45041, #80972, #132600, .T. ) ;
#136898=CARTESIAN_POINT ( 'NONE',  ( -19.35292824042819504, -2.786763769301527027, 4.186878071398595580 ) ) ;
#136899=ORIENTED_EDGE ( 'NONE', *, *, #117930, .T. ) ;
#136901=ORIENTED_EDGE ( 'NONE', *, *, #136846, .F. ) ;
#136902=CARTESIAN_POINT ( 'NONE',  ( 9.183988606268997046, 28.73617430169793607, 5.000000000000000000 ) ) ;
#136903=VECTOR ( 'NONE', #80174, 1000.000000000000000 ) ;
#136905=FACE_OUTER_BOUND ( 'NONE', #5052, .T. ) ;
#136907=EDGE_LOOP ( 'NONE', ( #93794, #141774, #122134, #62463 ) ) ;
#136908=ORIENTED_EDGE ( 'NONE', *, *, #107557, .T. ) ;
#136910=ORIENTED_EDGE ( 'NONE', *, *, #18722, .F. ) ;
#136912=CARTESIAN_POINT ( 'NONE',  ( -7.499999999999944045, 9.052185695429077583, 5.000000000000000000 ) ) ;
#136914=CARTESIAN_POINT ( 'NONE',  ( -33.18398860626899705, 28.73617430169810305, 5.000000000000000000 ) ) ;
#136915=ORIENTED_EDGE ( 'NONE', *, *, #67297, .T. ) ;
#136916=DIRECTION ( 'NONE',  ( 0.6830127018922180770, -0.6830127018922204085, -0.2588190451025213501 ) ) ;
#136917=CARTESIAN_POINT ( 'NONE',  ( 12.18398860626900060, 28.73617430169795739, 5.000000000000000000 ) ) ;
#136918=DIRECTION ( 'NONE',  ( -0.7071067811865487940, 0.7071067811865463515, 0.000000000000000000 ) ) ;
#136919=PLANE ( 'NONE',  #37316 ) ;
#136920=DIRECTION ( 'NONE',  ( -0.000000000000000000, 0.3543493200069153248, 0.9351131265310292928 ) ) ;
#136921=AXIS2_PLACEMENT_3D ( 'NONE', #86169, #73860, #65879 ) ;
#136923=LINE ( 'NONE', #128891, #51005 ) ;
#136924=AXIS2_PLACEMENT_3D ( 'NONE', #73288, #119595, #31907 ) ;
#136925=PLANE ( 'NONE',  #125788 ) ;
#136926=ORIENTED_EDGE ( 'NONE', *, *, #104016, .T. ) ;
#136927=LINE ( 'NONE', #5672, #134013 ) ;
#136929=VERTEX_POINT ( 'NONE', #64446 ) ;
#136930=ORIENTED_EDGE ( 'NONE', *, *, #8739, .F. ) ;
#136932=LINE ( 'NONE', #73648, #142736 ) ;
#136933=DIRECTION ( 'NONE',  ( -0.3543493200069163240, 0.000000000000000000, 0.9351131265310288487 ) ) ;
#136935=ORIENTED_EDGE ( 'NONE', *, *, #92222, .F. ) ;
#136936=DIRECTION ( 'NONE',  ( 0.7071067811865486830, -0.7071067811865464625, -0.000000000000000000 ) ) ;
#136937=PLANE ( 'NONE',  #10500 ) ;
#136938=DIRECTION ( 'NONE',  ( -0.3543493200069162685, -0.000000000000000000, -0.9351131265310288487 ) ) ;
#136940=EDGE_CURVE ( 'NONE', #40695, #29533, #87628, .T. ) ;
#136941=CARTESIAN_POINT ( 'NONE',  ( 9.489213562373095101, -27.52281430457062328, 5.000000000000000000 ) ) ;
#136942=CARTESIAN_POINT ( 'NONE',  ( -8.510786437626906675, -27.52281430457049183, 5.000000000000000000 ) ) ;
#136943=EDGE_CURVE ( 'NONE', #136524, #67529, #100662, .T. ) ;
#136944=CARTESIAN_POINT ( 'NONE',  ( -51.48921356237309510, -27.52281430457091460, 5.000000000000000000 ) ) ;
#136945=CARTESIAN_POINT ( 'NONE',  ( 4.171830600776447184, 3.759292476615678336, 4.000000000000000000 ) ) ;
#136946=EDGE_CURVE ( 'NONE', #89301, #14297, #56484, .T. ) ;
#136950=CARTESIAN_POINT ( 'NONE',  ( -2.292893218813436107, -18.74070752338409562, 5.000000000000000000 ) ) ;
#136952=CARTESIAN_POINT ( 'NONE',  ( 7.499999999999947597, -13.53360074219760101, 5.000000000000000000 ) ) ;
#136953=DIRECTION ( 'NONE',  ( -0.000000000000000000, 0.000000000000000000, 1.000000000000000000 ) ) ;
#136954=ADVANCED_FACE ( 'NONE', ( #78196 ), #76044, .F. ) ;
#136956=ORIENTED_EDGE ( 'NONE', *, *, #49939, .F. ) ;
#136957=VECTOR ( 'NONE', #82175, 1000.000000000000227 ) ;
#136959=VECTOR ( 'NONE', #123677, 1000.000000000000000 ) ;
#136960=ORIENTED_EDGE ( 'NONE', *, *, #132464, .T. ) ;
#136961=ORIENTED_EDGE ( 'NONE', *, *, #35061, .F. ) ;
#136962=CARTESIAN_POINT ( 'NONE',  ( 13.49999999999991296, -4.912538124160707120, 4.000000000000000000 ) ) ;
#136963=DIRECTION ( 'NONE',  ( 0.7071067811865486830, -0.7071067811865464625, -0.000000000000000000 ) ) ;
#136964=VECTOR ( 'NONE', #136032, 1000.000000000000000 ) ;
#136965=AXIS2_PLACEMENT_3D ( 'NONE', #47681, #93279, #102018 ) ;
#136968=ORIENTED_EDGE ( 'NONE', *, *, #10758, .T. ) ;
#136969=DIRECTION ( 'NONE',  ( -0.7071067811865486830, -0.7071067811865464625, 0.000000000000000000 ) ) ;
#136970=VECTOR ( 'NONE', #20274, 999.9999999999998863 ) ;
#136971=DIRECTION ( 'NONE',  ( 0.6830127018922181881, 0.6830127018922202975, -0.2588190451025214056 ) ) ;
#136972=EDGE_CURVE ( 'NONE', #128651, #127270, #86928, .T. ) ;
#136973=LINE ( 'NONE', #26773, #20954 ) ;
#136975=EDGE_CURVE ( 'NONE', #15400, #78073, #63582, .T. ) ;
#136976=DIRECTION ( 'NONE',  ( 0.3543493200069162685, -0.000000000000000000, -0.9351131265310288487 ) ) ;
#136977=DIRECTION ( 'NONE',  ( -0.000000000000000000, 0.000000000000000000, 1.000000000000000000 ) ) ;
#136978=DIRECTION ( 'NONE',  ( -0.000000000000000000, 0.000000000000000000, 1.000000000000000000 ) ) ;
#136979=CARTESIAN_POINT ( 'NONE',  ( -33.48921356237309510, -27.52281430457078670, 5.000000000000000000 ) ) ;
#136980=LINE ( 'NONE', #134873, #46960 ) ;
#136981=CARTESIAN_POINT ( 'NONE',  ( 34.92499999999998295, 12.95788372223795193, 1.488343219358033487 ) ) ;
#136982=FACE_OUTER_BOUND ( 'NONE', #46225, .T. ) ;
#136984=CARTESIAN_POINT ( 'NONE',  ( 11.70025512860841133, -27.71228299555198049, 4.000000000000000000 ) ) ;
#136986=VERTEX_POINT ( 'NONE', #21665 ) ;
#136988=ORIENTED_EDGE ( 'NONE', *, *, #35430, .T. ) ;
#136989=DIRECTION ( 'NONE',  ( 0.7071067811865487940, -0.7071067811865463515, 0.000000000000000000 ) ) ;
#136990=ADVANCED_FACE ( 'NONE', ( #55732 ), #10748, .F. ) ;
#136991=CARTESIAN_POINT ( 'NONE',  ( -39.48921356237310221, -27.52281430457082934, 5.000000000000000000 ) ) ;
#136993=DIRECTION ( 'NONE',  ( 1.000000000000000000, 0.000000000000000000, 0.000000000000000000 ) ) ;
#136994=DIRECTION ( 'NONE',  ( 0.7071067811865487940, -0.7071067811865463515, 0.000000000000000000 ) ) ;
#136998=ORIENTED_EDGE ( 'NONE', *, *, #106186, .F. ) ;
#136999=AXIS2_PLACEMENT_3D ( 'NONE', #5269, #24368, #127066 ) ;
#137001=DIRECTION ( 'NONE',  ( -0.6830127018922181881, 0.6830127018922202975, -0.2588190451025214056 ) ) ;
#137002=EDGE_CURVE ( 'NONE', #85826, #126030, #142725, .T. ) ;
#137003=DIRECTION ( 'NONE',  ( 0.7071067811865487940, 0.7071067811865463515, 0.000000000000000000 ) ) ;
#137004=VECTOR ( 'NONE', #42146, 1000.000000000000000 ) ;
#137005=DIRECTION ( 'NONE',  ( 1.000000000000000000, 0.000000000000000000, 0.000000000000000000 ) ) ;
#137007=ORIENTED_EDGE ( 'NONE', *, *, #88009, .T. ) ;
#137009=PLANE ( 'NONE',  #76964 ) ;
#137010=VECTOR ( 'NONE', #13987, 1000.000000000000000 ) ;
#137011=EDGE_CURVE ( 'NONE', #63240, #44164, #65915, .T. ) ;
#137013=CARTESIAN_POINT ( 'NONE',  ( 13.40832548098992660, -0.7407075233842701500, 14.76736230305383479 ) ) ;
#137015=ORIENTED_EDGE ( 'NONE', *, *, #1702, .F. ) ;
#137016=LINE ( 'NONE', #135599, #61788 ) ;
#137017=EDGE_CURVE ( 'NONE', #28064, #119026, #131138, .T. ) ;
#137018=VERTEX_POINT ( 'NONE', #120214 ) ;
#137019=ORIENTED_EDGE ( 'NONE', *, *, #48230, .F. ) ;
#137020=VECTOR ( 'NONE', #104333, 1000.000000000000227 ) ;
#137021=VECTOR ( 'NONE', #8684, 1000.000000000000000 ) ;
#137022=DIRECTION ( 'NONE',  ( 0.6830127018922180770, -0.6830127018922204085, -0.2588190451025213501 ) ) ;
#137023=CARTESIAN_POINT ( 'NONE',  ( 34.49999999999975842, -4.796895815300992183, -3.611700055028602918 ) ) ;
#137024=ORIENTED_EDGE ( 'NONE', *, *, #107449, .F. ) ;
#137025=DIRECTION ( 'NONE',  ( -0.7071067811865486830, -0.7071067811865464625, 0.000000000000000000 ) ) ;
#137026=ADVANCED_FACE ( 'NONE', ( #109376 ), #43417, .T. ) ;
#137028=CARTESIAN_POINT ( 'NONE',  ( 20.99999999999985079, -8.731860332648823331, -2.120594902707488405 ) ) ;
#137029=DIRECTION ( 'NONE',  ( -0.7071067811865486830, 0.7071067811865464625, 0.000000000000000000 ) ) ;
#137030=CARTESIAN_POINT ( 'NONE',  ( 23.99451991528749062, 28.92564299267954908, 4.000000000000000000 ) ) ;
#137031=FACE_BOUND ( 'NONE', #106058, .T. ) ;
#137032=ORIENTED_EDGE ( 'NONE', *, *, #35415, .F. ) ;
#137033=CARTESIAN_POINT ( 'NONE',  ( 20.29289321881331531, 11.25929247661560240, 5.000000000000000000 ) ) ;
#137034=CARTESIAN_POINT ( 'NONE',  ( 11.99999999999991829, -9.412538124160660047, 4.000000000000000000 ) ) ;
#137036=PLANE ( 'NONE',  #118630 ) ;
#137037=ORIENTED_EDGE ( 'NONE', *, *, #95485, .F. ) ;
#137038=DIRECTION ( 'NONE',  ( -0.000000000000000000, -0.000000000000000000, 1.000000000000000000 ) ) ;
#137039=VERTEX_POINT ( 'NONE', #600 ) ;
#137040=ORIENTED_EDGE ( 'NONE', *, *, #6760, .T. ) ;
#137041=AXIS2_PLACEMENT_3D ( 'NONE', #108212, #41557, #6220 ) ;
#137042=ORIENTED_EDGE ( 'NONE', *, *, #36171, .T. ) ;
#137044=VERTEX_POINT ( 'NONE', #68761 ) ;
#137046=CARTESIAN_POINT ( 'NONE',  ( -34.92500000000001137, 22.22500000000000142, 4.000000000000000000 ) ) ;
#137047=LINE ( 'NONE', #81993, #65990 ) ;
#137048=EDGE_CURVE ( 'NONE', #7797, #133878, #102080, .T. ) ;
#137049=ORIENTED_EDGE ( 'NONE', *, *, #93971, .T. ) ;
#137052=VECTOR ( 'NONE', #118368, 1000.000000000000000 ) ;
#137053=VECTOR ( 'NONE', #133513, 1000.000000000000000 ) ;
#137056=DIRECTION ( 'NONE',  ( -0.6830127018922181881, 0.6830127018922202975, -0.2588190451025214056 ) ) ;
#137057=FACE_OUTER_BOUND ( 'NONE', #98728, .T. ) ;
#137060=DIRECTION ( 'NONE',  ( -0.3543493200069162685, -0.000000000000000000, -0.9351131265310288487 ) ) ;
#137063=VECTOR ( 'NONE', #98291, 999.9999999999998863 ) ;
#137064=VERTEX_POINT ( 'NONE', #26654 ) ;
#137069=VERTEX_POINT ( 'NONE', #46309 ) ;
#137070=ORIENTED_EDGE ( 'NONE', *, *, #1736, .T. ) ;
#137071=CARTESIAN_POINT ( 'NONE',  ( 23.37053679528800743, 22.22500000000000142, -17.09035809333496658 ) ) ;
#137073=ADVANCED_FACE ( 'NONE', ( #1996 ), #91233, .F. ) ;
#137074=EDGE_CURVE ( 'NONE', #134215, #816, #47738, .T. ) ;
#137075=LINE ( 'NONE', #58855, #4539 ) ;
#137076=VERTEX_POINT ( 'NONE', #89760 ) ;
#137078=ORIENTED_EDGE ( 'NONE', *, *, #91890, .T. ) ;
#137079=CARTESIAN_POINT ( 'NONE',  ( 25.88982677111770769, -22.22500000000000853, 4.785647885939352975 ) ) ;
#137082=ORIENTED_EDGE ( 'NONE', *, *, #26787, .F. ) ;
#137084=LINE ( 'NONE', #124772, #121663 ) ;
#137085=CARTESIAN_POINT ( 'NONE',  ( -8.999999999999930722, -9.412538124160660047, 4.000000000000000000 ) ) ;
#137086=ORIENTED_EDGE ( 'NONE', *, *, #119329, .T. ) ;
#137088=DIRECTION ( 'NONE',  ( -0.7071067811865487940, 0.7071067811865463515, -0.000000000000000000 ) ) ;
#137089=VERTEX_POINT ( 'NONE', #37548 ) ;
#137090=DIRECTION ( 'NONE',  ( 1.000000000000000000, 0.000000000000000000, 0.000000000000000000 ) ) ;
#137092=FACE_OUTER_BOUND ( 'NONE', #44382, .T. ) ;
#137093=DIRECTION ( 'NONE',  ( -0.000000000000000000, -0.3543493200069152693, 0.9351131265310292928 ) ) ;
#137094=CARTESIAN_POINT ( 'NONE',  ( -24.32816939922335564, -6.740707523384212863, 4.000000000000000000 ) ) ;
#137095=ADVANCED_FACE ( 'NONE', ( #134739 ), #12904, .F. ) ;
#137096=ORIENTED_EDGE ( 'NONE', *, *, #121467, .T. ) ;
#137098=DIRECTION ( 'NONE',  ( 0.7071067811865486830, -0.7071067811865464625, -0.000000000000000000 ) ) ;
#137099=AXIS2_PLACEMENT_3D ( 'NONE', #24861, #69104, #103138 ) ;
#137100=VECTOR ( 'NONE', #126876, 999.9999999999998863 ) ;
#137102=CARTESIAN_POINT ( 'NONE',  ( 34.92499999999998295, 22.22500000000000142, 4.000000000000000000 ) ) ;
#137103=ORIENTED_EDGE ( 'NONE', *, *, #46361, .F. ) ;
#137104=DIRECTION ( 'NONE',  ( -0.7071067811865487940, 0.7071067811865463515, 0.000000000000000000 ) ) ;
#137106=CARTESIAN_POINT ( 'NONE',  ( -12.79289321881336683, -17.24070752338410628, 5.000000000000000000 ) ) ;
#137107=EDGE_LOOP ( 'NONE', ( #33503, #11619, #88125, #118150 ) ) ;
#137109=ORIENTED_EDGE ( 'NONE', *, *, #5322, .F. ) ;
#137110=EDGE_LOOP ( 'NONE', ( #45007, #94997, #66811, #125925 ) ) ;
#137111=CARTESIAN_POINT ( 'NONE',  ( 6.758600742197917732, 21.72500000000000142, 5.000000000000000000 ) ) ;
#137114=EDGE_LOOP ( 'NONE', ( #71599, #84190, #95407, #124064 ) ) ;
#137116=DIRECTION ( 'NONE',  ( 0.6830127018922181881, 0.6830127018922202975, -0.2588190451025214056 ) ) ;
#137117=ADVANCED_FACE ( 'NONE', ( #80352 ), #45589, .T. ) ;
#137118=DIRECTION ( 'NONE',  ( -0.7071067811865486830, 0.7071067811865464625, 0.000000000000000000 ) ) ;
#137119=VERTEX_POINT ( 'NONE', #133995 ) ;
#137120=DIRECTION ( 'NONE',  ( 0.3543493200069162685, -0.000000000000000000, -0.9351131265310288487 ) ) ;
#137122=CARTESIAN_POINT ( 'NONE',  ( -65.99451991528749772, 28.92564299267984396, 4.000000000000000000 ) ) ;
#137124=VECTOR ( 'NONE', #86568, 1000.000000000000227 ) ;
#137125=CARTESIAN_POINT ( 'NONE',  ( 1.828169399223516400, 9.759292476615625489, 4.000000000000000000 ) ) ;
#137126=PLANE ( 'NONE',  #3107 ) ;
#137127=VECTOR ( 'NONE', #47839, 1000.000000000000000 ) ;
#137128=CARTESIAN_POINT ( 'NONE',  ( -21.16696429985206152, -22.22500000000000142, 10.21343402916774146 ) ) ;
#137129=CARTESIAN_POINT ( 'NONE',  ( -15.87485380690756287, -14.24070752338414003, 9.401115078912694045 ) ) ;
#137130=CARTESIAN_POINT ( 'NONE',  ( -13.95484226663325167, -21.74070752338406720, 21.72585301388581769 ) ) ;
#137131=EDGE_CURVE ( 'NONE', #104041, #91273, #114374, .T. ) ;
#137132=EDGE_LOOP ( 'NONE', ( #15710, #41063, #75757, #24923 ) ) ;
#137133=EDGE_CURVE ( 'NONE', #61052, #87228, #136124, .T. ) ;
#137134=VERTEX_POINT ( 'NONE', #103477 ) ;
#137137=ORIENTED_EDGE ( 'NONE', *, *, #123807, .T. ) ;
#137138=VERTEX_POINT ( 'NONE', #36810 ) ;
#137139=ORIENTED_EDGE ( 'NONE', *, *, #76609, .T. ) ;
#137140=AXIS2_PLACEMENT_3D ( 'NONE', #141373, #84179, #86993 ) ;
#137141=LINE ( 'NONE', #50136, #45599 ) ;
#137142=DIRECTION ( 'NONE',  ( -0.7071067811865486830, -0.7071067811865464625, 0.000000000000000000 ) ) ;
#137143=VECTOR ( 'NONE', #52126, 1000.000000000000000 ) ;
#137144=ORIENTED_EDGE ( 'NONE', *, *, #76, .T. ) ;
#137145=CARTESIAN_POINT ( 'NONE',  ( -16.49999999999988276, 18.05218569542898521, 5.000000000000000000 ) ) ;
#137146=CARTESIAN_POINT ( 'NONE',  ( 0.000000000000000000, 0.000000000000000000, 5.000000000000000000 ) ) ;
#137147=EDGE_CURVE ( 'NONE', #32788, #49753, #81057, .T. ) ;
#137150=VERTEX_POINT ( 'NONE', #78923 ) ;
#137153=CARTESIAN_POINT ( 'NONE',  ( -34.92500000000001137, -14.99387692260790494, 4.000000000000000000 ) ) ;
#137154=FACE_OUTER_BOUND ( 'NONE', #142740, .T. ) ;
#137156=PLANE ( 'NONE',  #136153 ) ;
#137158=FACE_OUTER_BOUND ( 'NONE', #34592, .T. ) ;
#137159=CARTESIAN_POINT ( 'NONE',  ( 34.42499999999998295, 22.22500000000000142, 5.000000000000000000 ) ) ;
#137161=EDGE_CURVE ( 'NONE', #88480, #4875, #70900, .T. ) ;
#137163=DIRECTION ( 'NONE',  ( -0.7071067811865486830, -0.7071067811865464625, 0.000000000000000000 ) ) ;
#137164=ORIENTED_EDGE ( 'NONE', *, *, #59264, .F. ) ;
#137167=ORIENTED_EDGE ( 'NONE', *, *, #126686, .F. ) ;
#137168=ORIENTED_EDGE ( 'NONE', *, *, #86334, .T. ) ;
#137169=LINE ( 'NONE', #116829, #30101 ) ;
#137170=FACE_OUTER_BOUND ( 'NONE', #61301, .T. ) ;
#137171=ORIENTED_EDGE ( 'NONE', *, *, #42786, .F. ) ;
#137172=VECTOR ( 'NONE', #92698, 1000.000000000000000 ) ;
#137173=EDGE_CURVE ( 'NONE', #23783, #45084, #1309, .T. ) ;
#137174=VECTOR ( 'NONE', #123908, 1000.000000000000227 ) ;
#137175=VECTOR ( 'NONE', #43770, 1000.000000000000000 ) ;
#137177=LINE ( 'NONE', #83515, #83911 ) ;
#137179=LINE ( 'NONE', #114679, #44326 ) ;
#137182=EDGE_LOOP ( 'NONE', ( #4625, #37988, #810, #107408 ) ) ;
#137183=CARTESIAN_POINT ( 'NONE',  ( -6.005480084712508493, 28.92564299267933947, 4.000000000000000000 ) ) ;
#137184=ORIENTED_EDGE ( 'NONE', *, *, #87866, .T. ) ;
#137186=EDGE_CURVE ( 'NONE', #6272, #7430, #97417, .T. ) ;
#137187=AXIS2_PLACEMENT_3D ( 'NONE', #26419, #15490, #59772 ) ;
#137188=( GEOMETRIC_REPRESENTATION_CONTEXT ( 3 ) GLOBAL_UNCERTAINTY_ASSIGNED_CONTEXT ( ( #12642 ) ) GLOBAL_UNIT_ASSIGNED_CONTEXT ( ( #107224, #61623, #82637 ) ) REPRESENTATION_CONTEXT ( 'NONE', 'WORKASPACE' ) );
#137189=DIRECTION ( 'NONE',  ( -0.6830127018922181881, 0.6830127018922202975, -0.2588190451025214056 ) ) ;
#137190=CARTESIAN_POINT ( 'NONE',  ( 19.93003974513579024, -0.7407075233842735917, 13.87443053587606201 ) ) ;
#137191=DIRECTION ( 'NONE',  ( 0.7071067811865487940, -0.7071067811865463515, 0.000000000000000000 ) ) ;
#137193=ORIENTED_EDGE ( 'NONE', *, *, #50246, .F. ) ;
#137194=VERTEX_POINT ( 'NONE', #19168 ) ;
#137195=PLANE ( 'NONE',  #109535 ) ;
#137196=FACE_OUTER_BOUND ( 'NONE', #45518, .T. ) ;
#137197=CARTESIAN_POINT ( 'NONE',  ( -23.99999999999983302, -10.77435723561696435, -9.972017380717172585 ) ) ;
#137198=EDGE_CURVE ( 'NONE', #1609, #90903, #51099, .T. ) ;
#137199=EDGE_CURVE ( 'NONE', #62063, #56865, #140242, .T. ) ;
#137200=EDGE_CURVE ( 'NONE', #15048, #33461, #19867, .T. ) ;
#137203=ORIENTED_EDGE ( 'NONE', *, *, #5394, .T. ) ;
#137205=DIRECTION ( 'NONE',  ( -2.781805975412905890E-17, 0.3543493200069152693, 0.9351131265310292928 ) ) ;
#137206=ORIENTED_EDGE ( 'NONE', *, *, #63803, .F. ) ;
#137208=CARTESIAN_POINT ( 'NONE',  ( -14.99999999999989519, 18.08204922493371924, 0.9627537363045218788 ) ) ;
#137209=ORIENTED_EDGE ( 'NONE', *, *, #29657, .F. ) ;
#137212=VECTOR ( 'NONE', #140988, 1000.000000000000000 ) ;
#137213=FACE_OUTER_BOUND ( 'NONE', #36142, .T. ) ;
#137214=DIRECTION ( 'NONE',  ( 0.7071067811865486830, -0.7071067811865464625, -0.000000000000000000 ) ) ;
#137215=AXIS2_PLACEMENT_3D ( 'NONE', #97368, #920, #54626 ) ;
#137216=CARTESIAN_POINT ( 'NONE',  ( -34.47516574401891631, 22.22311076525683760, 4.292435211493030423 ) ) ;
#137217=FACE_BOUND ( 'NONE', #74356, .T. ) ;
#137218=CARTESIAN_POINT ( 'NONE',  ( 48.48921356237309510, -27.52281430457089328, 5.000000000000000000 ) ) ;
#137220=CARTESIAN_POINT ( 'NONE',  ( -34.92500000000001137, -22.22500000000000142, 4.000000000000000000 ) ) ;
#137221=FACE_OUTER_BOUND ( 'NONE', #87407, .T. ) ;
#137222=DIRECTION ( 'NONE',  ( 0.7071067811865487940, 0.7071067811865463515, -0.000000000000000000 ) ) ;
#137223=ORIENTED_EDGE ( 'NONE', *, *, #55785, .T. ) ;
#137224=CARTESIAN_POINT ( 'NONE',  ( -11.99999999999990230, 20.58746187583903264, 4.000000000000000000 ) ) ;
#137225=ORIENTED_EDGE ( 'NONE', *, *, #140217, .T. ) ;
#137226=EDGE_LOOP ( 'NONE', ( #97051, #9097, #112959, #122844 ) ) ;
#137229=DIRECTION ( 'NONE',  ( -0.6830127018922180770, -0.6830127018922204085, -0.2588190451025213501 ) ) ;
#137230=DIRECTION ( 'NONE',  ( 1.000000000000000000, 0.000000000000000000, 0.000000000000000000 ) ) ;
#137231=AXIS2_PLACEMENT_3D ( 'NONE', #5222, #127010, #95101 ) ;
#137233=DIRECTION ( 'NONE',  ( -0.6830127018922181881, 0.6830127018922202975, -0.2588190451025214056 ) ) ;
#137234=VECTOR ( 'NONE', #11959, 1000.000000000000000 ) ;
#137235=( BOUNDED_CURVE ( )  B_SPLINE_CURVE ( 3, ( #108388, #141802, #86705, #73672 ),
 .UNSPECIFIED., .F., .F. ) 
 B_SPLINE_CURVE_WITH_KNOTS ( ( 4, 4 ),
 ( 1.248621635838844446, 1.295595743666722033 ),
 .UNSPECIFIED. ) 
 CURVE ( )  GEOMETRIC_REPRESENTATION_ITEM ( )  RATIONAL_B_SPLINE_CURVE ( ( 1.000000000000000000, 0.9998161278856747547, 0.9998161278856747547, 1.000000000000000000 ) ) 
 REPRESENTATION_ITEM ( '' )  );
#137236=CARTESIAN_POINT ( 'NONE',  ( -26.99451991528749417, 28.92564299267956685, 4.000000000000000000 ) ) ;
#137237=LINE ( 'NONE', #3804, #45915 ) ;
#137238=CARTESIAN_POINT ( 'NONE',  ( -11.20710678118646442, 3.759292476615676559, 5.000000000000000000 ) ) ;
#137239=CARTESIAN_POINT ( 'NONE',  ( -5.816011393731002066, 28.73617430169783304, 5.000000000000000000 ) ) ;
#137243=VERTEX_POINT ( 'NONE', #131507 ) ;
#137244=DIRECTION ( 'NONE',  ( 0.7071067811865487940, -0.7071067811865463515, 0.000000000000000000 ) ) ;
#137245=( BOUNDED_CURVE ( )  B_SPLINE_CURVE ( 3, ( #50675, #39089, #94868, #127520 ),
 .UNSPECIFIED., .F., .T. ) 
 B_SPLINE_CURVE_WITH_KNOTS ( ( 4, 4 ),
 ( 4.407062196515976638, 4.453802039120700940 ),
 .UNSPECIFIED. ) 
 CURVE ( )  GEOMETRIC_REPRESENTATION_ITEM ( )  RATIONAL_B_SPLINE_CURVE ( ( 1.000000000000000000, 0.9998179572116046021, 0.9998179572116046021, 1.000000000000000000 ) ) 
 REPRESENTATION_ITEM ( '' )  );
#137246=DIRECTION ( 'NONE',  ( -0.7071067811865486830, -0.7071067811865464625, 0.000000000000000000 ) ) ;
#137248=ORIENTED_EDGE ( 'NONE', *, *, #113549, .F. ) ;
#137249=ORIENTED_EDGE ( 'NONE', *, *, #2516, .T. ) ;
#137250=DIRECTION ( 'NONE',  ( -1.000000000000000000, 0.000000000000000000, 0.000000000000000000 ) ) ;
#137251=CARTESIAN_POINT ( 'NONE',  ( -31.26506670282031664, 12.75929247661558996, 18.34774599283963425 ) ) ;
#137253=EDGE_CURVE ( 'NONE', #33632, #70176, #83018, .T. ) ;
#137254=DIRECTION ( 'NONE',  ( -0.7071067811865486830, -0.7071067811865464625, -0.000000000000000000 ) ) ;
#137255=VECTOR ( 'NONE', #30351, 1000.000000000000227 ) ;
#137256=ORIENTED_EDGE ( 'NONE', *, *, #17929, .F. ) ;
#137257=CARTESIAN_POINT ( 'NONE',  ( 22.49999999999984723, 21.05218569542895324, 5.000000000000000000 ) ) ;
#137259=CARTESIAN_POINT ( 'NONE',  ( -0.4892135623730947680, -27.52281430457055578, 5.000000000000000000 ) ) ;
#137260=EDGE_LOOP ( 'NONE', ( #109768, #33685, #64617, #134357 ) ) ;
#137261=EDGE_CURVE ( 'NONE', #24914, #4889, #142392, .T. ) ;
#137262=PLANE ( 'NONE',  #52671 ) ;
#137263=CARTESIAN_POINT ( 'NONE',  ( -6.156123077392362752, -22.22500000000000142, 4.000000000000000000 ) ) ;
#137264=DIRECTION ( 'NONE',  ( -0.000000000000000000, 0.3543493200069153248, 0.9351131265310292928 ) ) ;
#137265=LINE ( 'NONE', #61178, #88890 ) ;
#137268=VERTEX_POINT ( 'NONE', #30028 ) ;
#137269=FACE_OUTER_BOUND ( 'NONE', #136010, .T. ) ;
#137271=VECTOR ( 'NONE', #10988, 1000.000000000000227 ) ;
#137274=VECTOR ( 'NONE', #20597, 1000.000000000000000 ) ;
#137275=VERTEX_POINT ( 'NONE', #106137 ) ;
#137276=LINE ( 'NONE', #37237, #103819 ) ;
#137277=CARTESIAN_POINT ( 'NONE',  ( -4.499999999999959144, -20.94781430457061333, 5.000000000000000000 ) ) ;
#137278=DIRECTION ( 'NONE',  ( -0.7071067811865486830, -0.7071067811865464625, 0.000000000000000000 ) ) ;
#137279=DIRECTION ( 'NONE',  ( -0.7071067811865487940, 0.7071067811865463515, 0.000000000000000000 ) ) ;
#137285=DIRECTION ( 'NONE',  ( 0.7071067811865487940, 0.7071067811865463515, -0.000000000000000000 ) ) ;
#137286=CARTESIAN_POINT ( 'NONE',  ( 33.48921356237309510, -27.52281430457078670, 5.000000000000000000 ) ) ;
#137288=FACE_OUTER_BOUND ( 'NONE', #24118, .T. ) ;
#137289=LINE ( 'NONE', #16926, #134038 ) ;
#137290=VERTEX_POINT ( 'NONE', #63426 ) ;
#137291=EDGE_LOOP ( 'NONE', ( #109814, #111204, #91298, #96433 ) ) ;
#137292=EDGE_CURVE ( 'NONE', #106881, #129256, #85844, .T. ) ;
#137296=LINE ( 'NONE', #37993, #124589 ) ;
#137297=VECTOR ( 'NONE', #142996, 1000.000000000000000 ) ;
#137298=PLANE ( 'NONE',  #71581 ) ;
#137299=PLANE ( 'NONE',  #138655 ) ;
#137300=DIRECTION ( 'NONE',  ( -0.000000000000000000, 0.3543493200069153248, 0.9351131265310292928 ) ) ;
#137301=ORIENTED_EDGE ( 'NONE', *, *, #5703, .T. ) ;
#137302=EDGE_CURVE ( 'NONE', #39873, #140739, #31480, .T. ) ;
#137303=LINE ( 'NONE', #5323, #99742 ) ;
#137304=DIRECTION ( 'NONE',  ( 0.7071067811865487940, 0.7071067811865463515, 0.000000000000000000 ) ) ;
#137305=DIRECTION ( 'NONE',  ( -0.000000000000000000, -0.3543493200069152693, 0.9351131265310292928 ) ) ;
#137309=ADVANCED_FACE ( 'NONE', ( #8252 ), #29317, .F. ) ;
#137310=EDGE_CURVE ( 'NONE', #62501, #134514, #75702, .T. ) ;
#137311=ORIENTED_EDGE ( 'NONE', *, *, #29931, .T. ) ;
#137312=DIRECTION ( 'NONE',  ( -4.681814790819591790E-17, -0.3543493200069152693, 0.9351131265310292928 ) ) ;
#137313=VECTOR ( 'NONE', #102526, 1000.000000000000000 ) ;
#137314=ORIENTED_EDGE ( 'NONE', *, *, #42681, .F. ) ;
#137315=ORIENTED_EDGE ( 'NONE', *, *, #13378, .T. ) ;
#137316=CARTESIAN_POINT ( 'NONE',  ( -26.67183060077628909, 11.25929247661560417, 4.000000000000000000 ) ) ;
#137317=ADVANCED_FACE ( 'NONE', ( #30781 ), #75006, .F. ) ;
#137318=CARTESIAN_POINT ( 'NONE',  ( -15.19713381108422290, 7.733989266307781385, 4.000000000000000000 ) ) ;
#137319=CARTESIAN_POINT ( 'NONE',  ( 8.816011393731004731, 28.73617430169781173, 5.000000000000000000 ) ) ;
#137320=DIRECTION ( 'NONE',  ( -0.6830127018922180770, -0.6830127018922204085, -0.2588190451025213501 ) ) ;
#137321=ADVANCED_FACE ( 'NONE', ( #130813 ), #119870, .T. ) ;
#137322=DIRECTION ( 'NONE',  ( 0.7071067811865487940, -0.7071067811865463515, 0.000000000000000000 ) ) ;
#137324=ORIENTED_EDGE ( 'NONE', *, *, #121425, .T. ) ;
#137325=ADVANCED_FACE ( 'NONE', ( #12559 ), #134370, .T. ) ;
#137326=CARTESIAN_POINT ( 'NONE',  ( -9.770042794577866729, 21.73644205237998150, 5.000000000000000000 ) ) ;
#137329=CARTESIAN_POINT ( 'NONE',  ( 0.000000000000000000, 0.000000000000000000, 5.000000000000000000 ) ) ;
#137330=FACE_OUTER_BOUND ( 'NONE', #42485, .T. ) ;
#137331=CARTESIAN_POINT ( 'NONE',  ( 19.49999999999986500, 10.46639925780215563, 5.000000000000000000 ) ) ;
#137332=VECTOR ( 'NONE', #72616, 1000.000000000000000 ) ;
#137334=DIRECTION ( 'NONE',  ( -0.7071067811865487940, 0.7071067811865463515, -0.000000000000000000 ) ) ;
#137335=ORIENTED_EDGE ( 'NONE', *, *, #112306, .T. ) ;
#137336=ORIENTED_EDGE ( 'NONE', *, *, #141730, .F. ) ;
#137338=ADVANCED_FACE ( 'NONE', ( #111899 ), #109741, .F. ) ;
#137339=CYLINDRICAL_SURFACE ( 'NONE', #93342, 0.5000000000000004441 ) ;
#137340=CARTESIAN_POINT ( 'NONE',  ( 27.18398860626900060, 28.73617430169806042, 5.000000000000000000 ) ) ;
#137341=LINE ( 'NONE', #80825, #31260 ) ;
#137343=VECTOR ( 'NONE', #114487, 999.9999999999998863 ) ;
#137344=VERTEX_POINT ( 'NONE', #56840 ) ;
#137345=EDGE_CURVE ( 'NONE', #129516, #45966, #99557, .T. ) ;
#137346=CARTESIAN_POINT ( 'NONE',  ( 20.99999999999985079, -10.77435723561693415, -9.972017380717277391 ) ) ;
#137350=ORIENTED_EDGE ( 'NONE', *, *, #39935, .F. ) ;
#137352=VECTOR ( 'NONE', #35302, 999.9999999999998863 ) ;
#137355=LINE ( 'NONE', #27858, #23440 ) ;
#137356=CARTESIAN_POINT ( 'NONE',  ( -8.510786437626906675, -27.52281430457049183, 5.000000000000000000 ) ) ;
#137357=CARTESIAN_POINT ( 'NONE',  ( 12.32816939922344268, 2.259292476615688994, 4.000000000000000000 ) ) ;
#137358=LINE ( 'NONE', #112732, #73046 ) ;
#137359=ORIENTED_EDGE ( 'NONE', *, *, #142080, .F. ) ;
#137360=CARTESIAN_POINT ( 'NONE',  ( -16.49999999999988276, -19.53360074219753884, 5.000000000000000000 ) ) ;
#137362=VECTOR ( 'NONE', #4618, 1000.000000000000227 ) ;
#137363=DIRECTION ( 'NONE',  ( 0.7071067811865487940, 0.7071067811865463515, -0.000000000000000000 ) ) ;
#137364=CARTESIAN_POINT ( 'NONE',  ( -39.18398860626899705, 28.73617430169814568, 5.000000000000000000 ) ) ;
#137365=EDGE_CURVE ( 'NONE', #110210, #18270, #87993, .T. ) ;
#137366=EDGE_LOOP ( 'NONE', ( #85386, #126306, #47725, #7899 ) ) ;
#137368=EDGE_LOOP ( 'NONE', ( #139973, #91101, #126781, #6589 ) ) ;
#137369=LINE ( 'NONE', #38059, #66205 ) ;
#137370=EDGE_CURVE ( 'NONE', #11670, #14791, #80014, .T. ) ;
#137373=FACE_OUTER_BOUND ( 'NONE', #135361, .T. ) ;
#137374=EDGE_LOOP ( 'NONE', ( #86034, #24360, #142468, #122551 ) ) ;
#137375=ORIENTED_EDGE ( 'NONE', *, *, #86243, .T. ) ;
#137376=VECTOR ( 'NONE', #138357, 999.9999999999998863 ) ;
#137377=CARTESIAN_POINT ( 'NONE',  ( 30.71757738642546798, -21.73023691814492508, 5.000000000000000000 ) ) ;
#137378=DIRECTION ( 'NONE',  ( 0.6830127018922180770, -0.6830127018922204085, -0.2588190451025213501 ) ) ;
#137379=EDGE_CURVE ( 'NONE', #64078, #88422, #57532, .T. ) ;
#137380=AXIS2_PLACEMENT_3D ( 'NONE', #120424, #129921, #76264 ) ;
#137381=VERTEX_POINT ( 'NONE', #1655 ) ;
#137382=PLANE ( 'NONE',  #69981 ) ;
#137383=ORIENTED_EDGE ( 'NONE', *, *, #19575, .F. ) ;
#137384=DIRECTION ( 'NONE',  ( 1.000000000000000000, 0.000000000000000000, 0.000000000000000000 ) ) ;
#137385=LINE ( 'NONE', #83001, #61019 ) ;
#137386=VECTOR ( 'NONE', #52300, 1000.000000000000227 ) ;
#137387=FACE_BOUND ( 'NONE', #91990, .T. ) ;
#137388=LINE ( 'NONE', #26475, #96465 ) ;
#137390=DIRECTION ( 'NONE',  ( -1.000000000000000000, 0.000000000000000000, -0.000000000000000000 ) ) ;
#137392=VECTOR ( 'NONE', #127398, 1000.000000000000000 ) ;
#137393=LINE ( 'NONE', #39521, #25558 ) ;
#137395=VERTEX_POINT ( 'NONE', #122024 ) ;
#137396=VECTOR ( 'NONE', #7287, 999.9999999999998863 ) ;
#137397=ORIENTED_EDGE ( 'NONE', *, *, #107169, .T. ) ;
#137400=CARTESIAN_POINT ( 'NONE',  ( -33.48921356237309510, -27.52281430457078670, 5.000000000000000000 ) ) ;
#137402=VECTOR ( 'NONE', #129386, 1000.000000000000000 ) ;
#137403=DIRECTION ( 'NONE',  ( -0.7071067811865486830, -0.7071067811865464625, 0.000000000000000000 ) ) ;
#137405=DIRECTION ( 'NONE',  ( 0.7071067811865487940, -0.7071067811865463515, 0.000000000000000000 ) ) ;
#137406=DIRECTION ( 'NONE',  ( 0.7071067811865487940, -0.7071067811865463515, 0.000000000000000000 ) ) ;
#137407=AXIS2_PLACEMENT_3D ( 'NONE', #12613, #122083, #44588 ) ;
#137408=CARTESIAN_POINT ( 'NONE',  ( -19.49999999999985789, 22.08746187583901843, 4.000000000000000000 ) ) ;
#137409=FACE_OUTER_BOUND ( 'NONE', #3655, .T. ) ;
#137411=CARTESIAN_POINT ( 'NONE',  ( -24.33010218547250503, 17.25929247661553845, 19.83885114516076698 ) ) ;
#137412=CARTESIAN_POINT ( 'NONE',  ( 17.01793588964200055, 8.788317580041921318, 4.329525704382067630 ) ) ;
#137413=CARTESIAN_POINT ( 'NONE',  ( -1.823340898400253263, 5.259292476615672562, 15.86257073897098380 ) ) ;
#137414=EDGE_LOOP ( 'NONE', ( #81297, #36773, #104203, #68831 ) ) ;
#137415=PLANE ( 'NONE',  #86588 ) ;
#137416=CARTESIAN_POINT ( 'NONE',  ( 36.48921356237310221, -27.52281430457080802, 5.000000000000000000 ) ) ;
#137417=VECTOR ( 'NONE', #11164, 1000.000000000000227 ) ;
#137418=EDGE_CURVE ( 'NONE', #77505, #127735, #101721, .T. ) ;
#137419=EDGE_LOOP ( 'NONE', ( #106245, #57657, #8117, #95466 ) ) ;
#137421=EDGE_CURVE ( 'NONE', #71177, #118545, #121324, .T. ) ;
#137422=EDGE_CURVE ( 'NONE', #89594, #120060, #45940, .T. ) ;
#137423=EDGE_LOOP ( 'NONE', ( #37547, #91234, #52569, #38841 ) ) ;
#137425=EDGE_LOOP ( 'NONE', ( #94705, #100316, #49697 ) ) ;
#137427=ADVANCED_FACE ( 'NONE', ( #11835 ), #11105, .F. ) ;
#137428=ADVANCED_FACE ( 'NONE', ( #43780 ), #66257, .F. ) ;
#137432=ORIENTED_EDGE ( 'NONE', *, *, #119105, .T. ) ;
#137433=EDGE_CURVE ( 'NONE', #32019, #19651, #33640, .T. ) ;
#137434=DIRECTION ( 'NONE',  ( -0.7071067811865486830, -0.7071067811865464625, -0.000000000000000000 ) ) ;
#137437=CARTESIAN_POINT ( 'NONE',  ( 1.031635159221905962, 2.259292476615694323, 13.77329220150637745 ) ) ;
#137438=ORIENTED_EDGE ( 'NONE', *, *, #73594, .T. ) ;
#137439=ORIENTED_EDGE ( 'NONE', *, *, #142163, .F. ) ;
#137440=CARTESIAN_POINT ( 'NONE',  ( 30.48921356237309510, -27.52281430457076894, 5.000000000000000000 ) ) ;
#137441=DIRECTION ( 'NONE',  ( -0.000000000000000000, 0.3543493200069153248, 0.9351131265310292928 ) ) ;
#137442=EDGE_CURVE ( 'NONE', #136324, #99127, #960, .T. ) ;
#137443=ORIENTED_EDGE ( 'NONE', *, *, #2516, .F. ) ;
#137445=VERTEX_POINT ( 'NONE', #133651 ) ;
#137446=VERTEX_POINT ( 'NONE', #34328 ) ;
#137447=ORIENTED_EDGE ( 'NONE', *, *, #131029, .T. ) ;
#137450=VECTOR ( 'NONE', #114927, 1000.000000000000227 ) ;
#137451=EDGE_CURVE ( 'NONE', #117979, #66120, #24168, .T. ) ;
#137452=CARTESIAN_POINT ( 'NONE',  ( -2.999999999999981792, -0.2811185226894372113, -5.995736974527509311 ) ) ;
#137453=CARTESIAN_POINT ( 'NONE',  ( -34.92500000000001137, -2.337538124160983610, 4.000000000000000000 ) ) ;
#137454=DIRECTION ( 'NONE',  ( -0.6830127018922180770, -0.6830127018922204085, -0.2588190451025213501 ) ) ;
#137455=AXIS2_PLACEMENT_3D ( 'NONE', #63397, #8223, #20539 ) ;
#137457=ADVANCED_FACE ( 'NONE', ( #137221 ), #70571, .F. ) ;
#137458=DIRECTION ( 'NONE',  ( -0.7071067811865486830, -0.7071067811865464625, 0.000000000000000000 ) ) ;
#137460=DIRECTION ( 'NONE',  ( -0.000000000000000000, 0.000000000000000000, 1.000000000000000000 ) ) ;
#137461=VECTOR ( 'NONE', #3308, 1000.000000000000000 ) ;
#137462=CARTESIAN_POINT ( 'NONE',  ( 23.58838509405153161, 22.22500000000000142, 4.777194822843816802 ) ) ;
#137463=FACE_OUTER_BOUND ( 'NONE', #115408, .T. ) ;
#137465=VERTEX_POINT ( 'NONE', #102464 ) ;
#137466=EDGE_CURVE ( 'NONE', #5145, #3084, #16101, .T. ) ;
#137467=ORIENTED_EDGE ( 'NONE', *, *, #33416, .F. ) ;
#137468=LINE ( 'NONE', #60657, #13944 ) ;
#137471=CARTESIAN_POINT ( 'NONE',  ( -54.18398860626899705, 28.73617430169825226, 5.000000000000000000 ) ) ;
#137472=CARTESIAN_POINT ( 'NONE',  ( 45.48921356237309510, -27.52281430457087197, 5.000000000000000000 ) ) ;
#137473=LINE ( 'NONE', #27253, #99125 ) ;
#137475=VECTOR ( 'NONE', #132644, 1000.000000000000000 ) ;
#137476=CARTESIAN_POINT ( 'NONE',  ( 25.49999999999982236, 21.43112307739196254, 4.000000000000000000 ) ) ;
#137477=EDGE_CURVE ( 'NONE', #20950, #65937, #69945, .T. ) ;
#137478=DIRECTION ( 'NONE',  ( -0.3543493200069162685, -0.000000000000000000, -0.9351131265310288487 ) ) ;
#137479=CARTESIAN_POINT ( 'NONE',  ( 66.18398860626901126, 28.73617430169833753, 5.000000000000000000 ) ) ;
#137480=CARTESIAN_POINT ( 'NONE',  ( -6.489213562373093325, -27.52281430457059841, 5.000000000000000000 ) ) ;
#137481=EDGE_CURVE ( 'NONE', #94597, #4103, #114715, .T. ) ;
#137482=CARTESIAN_POINT ( 'NONE',  ( -12.18398860626900060, 28.73617430169795739, 5.000000000000000000 ) ) ;
#137483=ORIENTED_EDGE ( 'NONE', *, *, #36727, .F. ) ;
#137484=CARTESIAN_POINT ( 'NONE',  ( -41.99451991528749062, 28.92564299267967343, 4.000000000000000000 ) ) ;
#137485=VERTEX_POINT ( 'NONE', #15389 ) ;
#137487=PLANE ( 'NONE',  #50600 ) ;
#137488=PLANE ( 'NONE',  #81213 ) ;
#137490=DIRECTION ( 'NONE',  ( -0.7071067811865486830, -0.7071067811865464625, 0.000000000000000000 ) ) ;
#137491=CARTESIAN_POINT ( 'NONE',  ( 17.99999999999986855, -19.44781430457062044, 5.000000000000000000 ) ) ;
#137492=ORIENTED_EDGE ( 'NONE', *, *, #84935, .F. ) ;
#137494=ORIENTED_EDGE ( 'NONE', *, *, #83883, .T. ) ;
#137496=ORIENTED_EDGE ( 'NONE', *, *, #67665, .F. ) ;
#137498=LINE ( 'NONE', #37477, #45033 ) ;
#137500=CARTESIAN_POINT ( 'NONE',  ( 53.99451991528749062, 28.92564299267975869, 4.000000000000000000 ) ) ;
#137501=VECTOR ( 'NONE', #23157, 1000.000000000000000 ) ;
#137502=ORIENTED_EDGE ( 'NONE', *, *, #45677, .T. ) ;
#137503=EDGE_CURVE ( 'NONE', #20582, #105080, #4480, .T. ) ;
#137507=DIRECTION ( 'NONE',  ( -0.6830127018922180770, -0.6830127018922204085, -0.2588190451025213501 ) ) ;
#137508=CARTESIAN_POINT ( 'NONE',  ( 20.36090904532357371, -2.649219295539896990, 4.327832195654623071 ) ) ;
#137509=VERTEX_POINT ( 'NONE', #27012 ) ;
#137510=ADVANCED_FACE ( 'NONE', ( #58277 ), #127028, .T. ) ;
#137511=CIRCLE ( 'NONE', #35608, 5.968999999999998529 ) ;
#137512=LINE ( 'NONE', #125198, #2618 ) ;
#137513=ORIENTED_EDGE ( 'NONE', *, *, #74699, .T. ) ;
#137516=DIRECTION ( 'NONE',  ( 0.7071067811865487940, -0.7071067811865463515, 0.000000000000000000 ) ) ;
#137518=PLANE ( 'NONE',  #27085 ) ;
#137519=ORIENTED_EDGE ( 'NONE', *, *, #89920, .T. ) ;
#137520=CARTESIAN_POINT ( 'NONE',  ( -28.49999999999979039, 16.08746187583907883, 4.000000000000000000 ) ) ;
#137521=AXIS2_PLACEMENT_3D ( 'NONE', #96327, #16658, #93517 ) ;
#137522=DIRECTION ( 'NONE',  ( 0.3543493200069162685, -0.000000000000000000, -0.9351131265310288487 ) ) ;
#137525=CARTESIAN_POINT ( 'NONE',  ( -75.18398860626899705, 28.73617430169839793, 5.000000000000000000 ) ) ;
#137526=CARTESIAN_POINT ( 'NONE',  ( -9.183988606268997046, 28.73617430169793607, 5.000000000000000000 ) ) ;
#137527=EDGE_CURVE ( 'NONE', #125882, #71945, #92992, .T. ) ;
#137528=CARTESIAN_POINT ( 'NONE',  ( -3.005480084712505828, 28.92564299267936079, 4.000000000000000000 ) ) ;
#137529=ORIENTED_EDGE ( 'NONE', *, *, #32698, .F. ) ;
#137531=LINE ( 'NONE', #49105, #77815 ) ;
#137533=CARTESIAN_POINT ( 'NONE',  ( 2.510786437626908008, -27.52281430457053446, 5.000000000000000000 ) ) ;
#137534=VECTOR ( 'NONE', #97818, 1000.000000000000000 ) ;
#137536=ORIENTED_EDGE ( 'NONE', *, *, #142369, .T. ) ;
#137537=ORIENTED_EDGE ( 'NONE', *, *, #99190, .F. ) ;
#137539=VECTOR ( 'NONE', #82895, 999.9999999999998863 ) ;
#137540=ORIENTED_EDGE ( 'NONE', *, *, #113271, .T. ) ;
#137541=LINE ( 'NONE', #26626, #28940 ) ;
#137542=LINE ( 'NONE', #60726, #61933 ) ;
#137543=VECTOR ( 'NONE', #88103, 1000.000000000000227 ) ;
#137544=DIRECTION ( 'NONE',  ( 0.6830127018922180770, -0.6830127018922204085, -0.2588190451025213501 ) ) ;
#137545=LINE ( 'NONE', #138973, #10699 ) ;
#137546=VERTEX_POINT ( 'NONE', #58991 ) ;
#137547=PLANE ( 'NONE',  #46839 ) ;
#137548=CARTESIAN_POINT ( 'NONE',  ( -4.171830600776438303, -20.24070752338407431, 4.000000000000000000 ) ) ;
#137550=AXIS2_PLACEMENT_3D ( 'NONE', #128333, #140602, #6478 ) ;
#137551=EDGE_CURVE ( 'NONE', #60350, #116152, #36471, .T. ) ;
#137552=EDGE_LOOP ( 'NONE', ( #90566, #137438, #30086, #10031 ) ) ;
#137553=DIRECTION ( 'NONE',  ( 0.7071067811865487940, -0.7071067811865463515, 0.000000000000000000 ) ) ;
#137554=DIRECTION ( 'NONE',  ( 0.6830127018922181881, 0.6830127018922202975, -0.2588190451025214056 ) ) ;
#137555=VECTOR ( 'NONE', #48471, 1000.000000000000227 ) ;
#137556=LINE ( 'NONE', #33110, #104836 ) ;
#137557=VERTEX_POINT ( 'NONE', #20397 ) ;
#137558=ORIENTED_EDGE ( 'NONE', *, *, #98474, .T. ) ;
#137559=DIRECTION ( 'NONE',  ( 1.000000000000000000, 0.000000000000000000, 0.000000000000000000 ) ) ;
#137560=EDGE_CURVE ( 'NONE', #20628, #44804, #30610, .T. ) ;
#137561=DIRECTION ( 'NONE',  ( -0.3543493200069162685, -0.000000000000000000, -0.9351131265310288487 ) ) ;
#137563=LINE ( 'NONE', #38246, #65057 ) ;
#137564=DIRECTION ( 'NONE',  ( 0.6830127018922180770, -0.6830127018922204085, -0.2588190451025213501 ) ) ;
#137565=DIRECTION ( 'NONE',  ( 0.6830127018922181881, 0.6830127018922202975, -0.2588190451025214056 ) ) ;
#137566=ORIENTED_EDGE ( 'NONE', *, *, #118806, .F. ) ;
#137568=EDGE_LOOP ( 'NONE', ( #36763, #138387, #135465, #140479 ) ) ;
#137569=ORIENTED_EDGE ( 'NONE', *, *, #84611, .F. ) ;
#137570=ORIENTED_EDGE ( 'NONE', *, *, #9643, .T. ) ;
#137572=CARTESIAN_POINT ( 'NONE',  ( -34.92500000000001137, 22.22500000000000142, 4.000000000000000000 ) ) ;
#137574=LINE ( 'NONE', #125264, #43622 ) ;
#137575=CARTESIAN_POINT ( 'NONE',  ( 0.000000000000000000, 0.000000000000000000, 5.000000000000000000 ) ) ;
#137577=EDGE_CURVE ( 'NONE', #124775, #22382, #52330, .T. ) ;
#137579=LINE ( 'NONE', #105623, #76900 ) ;
#137580=ORIENTED_EDGE ( 'NONE', *, *, #58965, .F. ) ;
#137582=FACE_OUTER_BOUND ( 'NONE', #106482, .T. ) ;
#137583=DIRECTION ( 'NONE',  ( -0.6830127018922181881, 0.6830127018922202975, -0.2588190451025214056 ) ) ;
#137585=DIRECTION ( 'NONE',  ( 0.7071067811865487940, -0.7071067811865463515, 0.000000000000000000 ) ) ;
#137586=VERTEX_POINT ( 'NONE', #142229 ) ;
#137589=ADVANCED_FACE ( 'NONE', ( #108826 ), #18241, .F. ) ;
#137590=CARTESIAN_POINT ( 'NONE',  ( -9.793339364578404371, 21.75929247661549581, 4.998822639870701856 ) ) ;
#137591=EDGE_LOOP ( 'NONE', ( #90086, #8800, #97078, #126813 ) ) ;
#137592=ORIENTED_EDGE ( 'NONE', *, *, #126311, .T. ) ;
#137594=VECTOR ( 'NONE', #74123, 999.9999999999998863 ) ;
#137595=ORIENTED_EDGE ( 'NONE', *, *, #89910, .F. ) ;
#137596=ADVANCED_FACE ( 'NONE', ( #53792 ), #61814, .F. ) ;
#137597=EDGE_CURVE ( 'NONE', #1418, #140272, #18996, .T. ) ;
#137598=PLANE ( 'NONE',  #44303 ) ;
#137599=VECTOR ( 'NONE', #109309, 999.9999999999998863 ) ;
#137600=DIRECTION ( 'NONE',  ( -0.7071067811865486830, -0.7071067811865464625, -0.000000000000000000 ) ) ;
#137603=CARTESIAN_POINT ( 'NONE',  ( -22.49999999999984013, -11.94781430457070392, 5.000000000000000000 ) ) ;
#137604=VECTOR ( 'NONE', #17136, 1000.000000000000000 ) ;
#137605=EDGE_CURVE ( 'NONE', #124676, #30730, #129171, .T. ) ;
#137607=DIRECTION ( 'NONE',  ( -0.6830127018922181881, 0.6830127018922202975, -0.2588190451025214056 ) ) ;
#137608=PLANE ( 'NONE',  #69522 ) ;
#137609=CARTESIAN_POINT ( 'NONE',  ( 9.489213562373095101, -27.52281430457062328, 5.000000000000000000 ) ) ;
#137610=ADVANCED_FACE ( 'NONE', ( #108110 ), #129898, .F. ) ;
#137611=DIRECTION ( 'NONE',  ( -0.7071067811865486830, -0.7071067811865464625, 0.000000000000000000 ) ) ;
#137612=DIRECTION ( 'NONE',  ( -0.000000000000000000, -0.3543493200069152693, 0.9351131265310292928 ) ) ;
#137614=EDGE_CURVE ( 'NONE', #7434, #61259, #8775, .T. ) ;
#137615=ORIENTED_EDGE ( 'NONE', *, *, #49381, .T. ) ;
#137617=VECTOR ( 'NONE', #41894, 1000.000000000000000 ) ;
#137618=PLANE ( 'NONE',  #109977 ) ;
#137619=ORIENTED_EDGE ( 'NONE', *, *, #74717, .T. ) ;
#137620=VERTEX_POINT ( 'NONE', #787 ) ;
#137621=LINE ( 'NONE', #38301, #3187 ) ;
#137622=ORIENTED_EDGE ( 'NONE', *, *, #45840, .T. ) ;
#137623=DIRECTION ( 'NONE',  ( 0.7071067811865487940, -0.7071067811865463515, 0.000000000000000000 ) ) ;
#137624=DIRECTION ( 'NONE',  ( 0.7071067811865487940, 0.7071067811865463515, -0.000000000000000000 ) ) ;
#137625=LINE ( 'NONE', #126708, #52570 ) ;
#137626=ADVANCED_FACE ( 'NONE', ( #34166 ), #101540, .T. ) ;
#137628=CARTESIAN_POINT ( 'NONE',  ( 16.49999999999988631, -17.94781430457065952, 5.000000000000000000 ) ) ;
#137629=DIRECTION ( 'NONE',  ( -0.000000000000000000, 0.3543493200069153248, 0.9351131265310292928 ) ) ;
#137630=ORIENTED_EDGE ( 'NONE', *, *, #77692, .T. ) ;
#137631=EDGE_LOOP ( 'NONE', ( #81680, #141759, #79712, #9930 ) ) ;
#137633=LINE ( 'NONE', #53267, #111699 ) ;
#137634=CIRCLE ( 'NONE', #132996, 0.5000000000000004441 ) ;
#137635=VECTOR ( 'NONE', #124945, 1000.000000000000000 ) ;
#137637=LINE ( 'NONE', #128872, #23854 ) ;
#137638=VECTOR ( 'NONE', #57968, 1000.000000000000000 ) ;
#137640=PLANE ( 'NONE',  #120679 ) ;
#137641=ORIENTED_EDGE ( 'NONE', *, *, #38086, .T. ) ;
#137643=EDGE_LOOP ( 'NONE', ( #112984, #83573, #25101, #83037 ) ) ;
#137644=DIRECTION ( 'NONE',  ( -0.7071067811865486830, -0.7071067811865464625, 0.000000000000000000 ) ) ;
#137646=CARTESIAN_POINT ( 'NONE',  ( -13.22850677138656472, 20.25929247661551358, 7.808871592221738211 ) ) ;
#137647=DIRECTION ( 'NONE',  ( -0.7071067811865486830, -0.7071067811865464625, 0.000000000000000000 ) ) ;
#137650=DIRECTION ( 'NONE',  ( -0.000000000000000000, -0.3543493200069152693, 0.9351131265310292928 ) ) ;
#137651=AXIS2_PLACEMENT_3D ( 'NONE', #27921, #4680, #29335 ) ;
#137652=EDGE_CURVE ( 'NONE', #22185, #115243, #78384, .T. ) ;
#137653=CARTESIAN_POINT ( 'NONE',  ( 34.92499999999998295, 7.701930566820908375, 4.500000000000000888 ) ) ;
#137654=DIRECTION ( 'NONE',  ( -0.7071067811865486830, -0.7071067811865464625, -0.000000000000000000 ) ) ;
#137655=CARTESIAN_POINT ( 'NONE',  ( 34.75611968250419181, -9.187065745292510854, 4.955485411084881164 ) ) ;
#137657=ORIENTED_EDGE ( 'NONE', *, *, #101327, .T. ) ;
#137658=CARTESIAN_POINT ( 'NONE',  ( -14.20710678118644132, -8.240707523384200428, 5.000000000000000000 ) ) ;
#137660=ORIENTED_EDGE ( 'NONE', *, *, #98533, .F. ) ;
#137661=EDGE_CURVE ( 'NONE', #132130, #9981, #68258, .T. ) ;
#137662=LINE ( 'NONE', #24072, #15885 ) ;
#137663=CARTESIAN_POINT ( 'NONE',  ( 0.000000000000000000, 0.000000000000000000, 5.000000000000000000 ) ) ;
#137664=VERTEX_POINT ( 'NONE', #131328 ) ;
#137666=CARTESIAN_POINT ( 'NONE',  ( -57.18398860626899705, 28.73617430169827358, 5.000000000000000000 ) ) ;
#137667=DIRECTION ( 'NONE',  ( -1.000000000000000000, 6.938893903907222067E-15, 0.000000000000000000 ) ) ;
#137668=CARTESIAN_POINT ( 'NONE',  ( 42.48921356237308800, -27.52281430457085065, 5.000000000000000000 ) ) ;
#137669=EDGE_LOOP ( 'NONE', ( #132341, #122524, #142210, #100341 ) ) ;
#137670=CARTESIAN_POINT ( 'NONE',  ( -21.48921356237309155, -27.52281430457070499, 5.000000000000000000 ) ) ;
#137672=EDGE_LOOP ( 'NONE', ( #4205, #45714, #129094, #133682 ) ) ;
#137673=EDGE_CURVE ( 'NONE', #77465, #12213, #121150, .T. ) ;
#137674=DIRECTION ( 'NONE',  ( -0.3543493200069162685, -0.000000000000000000, -0.9351131265310288487 ) ) ;
#137678=DIRECTION ( 'NONE',  ( 0.7071067811865487940, 0.7071067811865463515, 0.000000000000000000 ) ) ;
#137679=ADVANCED_FACE ( 'NONE', ( #123334 ), #11651, .F. ) ;
#137680=DIRECTION ( 'NONE',  ( -0.6830127018922181881, 0.6830127018922202975, -0.2588190451025214056 ) ) ;
#137681=DIRECTION ( 'NONE',  ( 0.7071067811865487940, 0.7071067811865463515, 0.000000000000000000 ) ) ;
#137682=CARTESIAN_POINT ( 'NONE',  ( -17.99999999999987566, -7.068876922607736368, 4.000000000000000000 ) ) ;
#137685=LINE ( 'NONE', #53322, #71413 ) ;
#137686=DIRECTION ( 'NONE',  ( -0.7071067811865486830, -0.7071067811865464625, 0.000000000000000000 ) ) ;
#137687=CARTESIAN_POINT ( 'NONE',  ( 6.005480084712508493, 28.92564299267933947, 4.000000000000000000 ) ) ;
#137688=ORIENTED_EDGE ( 'NONE', *, *, #36182, .F. ) ;
#137690=ORIENTED_EDGE ( 'NONE', *, *, #59090, .F. ) ;
#137692=EDGE_LOOP ( 'NONE', ( #32198, #2829, #125599, #22779 ) ) ;
#137693=EDGE_LOOP ( 'NONE', ( #48216, #42767, #107962, #80404 ) ) ;
#137694=EDGE_CURVE ( 'NONE', #141201, #84993, #32749, .T. ) ;
#137696=LINE ( 'NONE', #50660, #101904 ) ;
#137697=CARTESIAN_POINT ( 'NONE',  ( -6.489213562373093325, -27.52281430457059841, 5.000000000000000000 ) ) ;
#137698=VERTEX_POINT ( 'NONE', #45080 ) ;
#137700=DIRECTION ( 'NONE',  ( -0.7071067811865486830, -0.7071067811865464625, 0.000000000000000000 ) ) ;
#137701=CARTESIAN_POINT ( 'NONE',  ( -78.29974487139158157, -27.71228299555260577, 4.000000000000000000 ) ) ;
#137703=ADVANCED_FACE ( 'NONE', ( #98683 ), #10244, .F. ) ;
#137704=DIRECTION ( 'NONE',  ( -0.7071067811865487940, 0.7071067811865463515, 0.000000000000000000 ) ) ;
#137705=DIRECTION ( 'NONE',  ( -0.7071067811865486830, 0.7071067811865464625, 0.000000000000000000 ) ) ;
#137706=DIRECTION ( 'NONE',  ( 0.7071067811865487940, -0.7071067811865463515, 0.000000000000000000 ) ) ;
#137707=DIRECTION ( 'NONE',  ( 0.7071067811865486830, -0.7071067811865464625, -0.000000000000000000 ) ) ;
#137708=PLANE ( 'NONE',  #44776 ) ;
#137709=CARTESIAN_POINT ( 'NONE',  ( 34.82816939922329169, 15.75929247661555976, 4.000000000000000000 ) ) ;
#137710=CARTESIAN_POINT ( 'NONE',  ( 0.000000000000000000, 0.000000000000000000, 5.000000000000000000 ) ) ;
#137711=CARTESIAN_POINT ( 'NONE',  ( -34.92500000000001137, -13.29806943317885448, 4.500000000000000888 ) ) ;
#137712=VECTOR ( 'NONE', #45717, 1000.000000000000000 ) ;
#137713=EDGE_CURVE ( 'NONE', #52975, #16650, #76242, .T. ) ;
#137714=ORIENTED_EDGE ( 'NONE', *, *, #43413, .T. ) ;
#137715=ORIENTED_EDGE ( 'NONE', *, *, #115636, .T. ) ;
#137717=ORIENTED_EDGE ( 'NONE', *, *, #124181, .F. ) ;
#137718=AXIS2_PLACEMENT_3D ( 'NONE', #51751, #95944, #138757 ) ;
#137719=LINE ( 'NONE', #37697, #54791 ) ;
#137720=CARTESIAN_POINT ( 'NONE',  ( 19.49999999999987210, -7.912538124160673370, 4.000000000000000000 ) ) ;
#137721=ORIENTED_EDGE ( 'NONE', *, *, #134375, .T. ) ;
#137723=LINE ( 'NONE', #40548, #81317 ) ;
#137724=EDGE_CURVE ( 'NONE', #88957, #11432, #48, .T. ) ;
#137726=EDGE_CURVE ( 'NONE', #54291, #76385, #89254, .T. ) ;
#137727=VECTOR ( 'NONE', #93239, 1000.000000000000000 ) ;
#137728=EDGE_LOOP ( 'NONE', ( #17823, #95608, #101296, #75929, #139415 ) ) ;
#137729=CARTESIAN_POINT ( 'NONE',  ( 39.29974487139159578, -27.71228299555233576, 4.000000000000000000 ) ) ;
#137730=VERTEX_POINT ( 'NONE', #65392 ) ;
#137731=DIRECTION ( 'NONE',  ( -0.000000000000000000, -0.3543493200069152693, 0.9351131265310292928 ) ) ;
#137732=CARTESIAN_POINT ( 'NONE',  ( -23.99999999999982947, -10.06887692260771239, 4.000000000000000000 ) ) ;
#137733=FACE_OUTER_BOUND ( 'NONE', #88877, .T. ) ;
#137734=ORIENTED_EDGE ( 'NONE', *, *, #7381, .F. ) ;
#137735=ORIENTED_EDGE ( 'NONE', *, *, #23702, .T. ) ;
#137736=EDGE_LOOP ( 'NONE', ( #132221, #128050, #129182, #95755 ) ) ;
#137737=LINE ( 'NONE', #93502, #97724 ) ;
#137738=ADVANCED_FACE ( 'NONE', ( #54505 ), #133480, .T. ) ;
#137741=LINE ( 'NONE', #45921, #78112 ) ;
#137742=VECTOR ( 'NONE', #75471, 1000.000000000000000 ) ;
#137745=ORIENTED_EDGE ( 'NONE', *, *, #104864, .F. ) ;
#137746=AXIS2_PLACEMENT_3D ( 'NONE', #113659, #91238, #124548 ) ;
#137747=ORIENTED_EDGE ( 'NONE', *, *, #44024, .T. ) ;
#137748=CARTESIAN_POINT ( 'NONE',  ( 20.91508676806225253, -12.74070752338414536, 18.74364270924359133 ) ) ;
#137749=ORIENTED_EDGE ( 'NONE', *, *, #126388, .F. ) ;
#137750=VERTEX_POINT ( 'NONE', #57364 ) ;
#137751=CARTESIAN_POINT ( 'NONE',  ( 18.18398860626898994, 28.73617430169800002, 5.000000000000000000 ) ) ;
#137752=LINE ( 'NONE', #47904, #32699 ) ;
#137753=DIRECTION ( 'NONE',  ( -0.7071067811865487940, 0.7071067811865463515, 0.000000000000000000 ) ) ;
#137754=ORIENTED_EDGE ( 'NONE', *, *, #106448, .T. ) ;
#137755=DIRECTION ( 'NONE',  ( -0.7071067811865487940, 0.7071067811865463515, 0.000000000000000000 ) ) ;
#137757=CARTESIAN_POINT ( 'NONE',  ( -32.22995720542186149, 21.73644205237997440, 5.000000000000000888 ) ) ;
#137758=CARTESIAN_POINT ( 'NONE',  ( 24.70710678118637915, 11.25929247661560240, 5.000000000000000000 ) ) ;
#137759=CARTESIAN_POINT ( 'NONE',  ( 10.49999999999993605, -1.912538124160735542, 4.000000000000000000 ) ) ;
#137760=ORIENTED_EDGE ( 'NONE', *, *, #128662, .T. ) ;
#137761=LINE ( 'NONE', #137030, #132116 ) ;
#137762=FACE_BOUND ( 'NONE', #49862, .T. ) ;
#137763=EDGE_LOOP ( 'NONE', ( #116418, #80650, #89707, #75251 ) ) ;
#137765=DIRECTION ( 'NONE',  ( -0.6830127018922180770, -0.6830127018922204085, -0.2588190451025213501 ) ) ;
#137767=EDGE_LOOP ( 'NONE', ( #13077, #54656, #40581, #1057 ) ) ;
#137768=DIRECTION ( 'NONE',  ( -0.7071067811865486830, -0.7071067811865464625, -0.000000000000000000 ) ) ;
#137769=ORIENTED_EDGE ( 'NONE', *, *, #28833, .T. ) ;
#137770=VERTEX_POINT ( 'NONE', #36304 ) ;
#137771=VERTEX_POINT ( 'NONE', #115233 ) ;
#137772=EDGE_CURVE ( 'NONE', #37438, #49326, #60959, .T. ) ;
#137774=ORIENTED_EDGE ( 'NONE', *, *, #27952, .F. ) ;
#137775=LINE ( 'NONE', #37753, #90021 ) ;
#137776=EDGE_CURVE ( 'NONE', #49544, #44266, #113126, .T. ) ;
#137777=CARTESIAN_POINT ( 'NONE',  ( 25.49999999999982236, -4.216083040037233332, -7.486842126848716639 ) ) ;
#137778=LINE ( 'NONE', #72559, #51990 ) ;
#137779=ADVANCED_FACE ( 'NONE', ( #27538 ), #16674, .F. ) ;
#137780=CARTESIAN_POINT ( 'NONE',  ( 29.99451991528749417, 28.92564299267958816, 4.000000000000000000 ) ) ;
#137782=EDGE_CURVE ( 'NONE', #23467, #140739, #115970, .T. ) ;
#137783=CARTESIAN_POINT ( 'NONE',  ( 1.499999999999984013, 12.43112307739206024, 4.000000000000000000 ) ) ;
#137784=DIRECTION ( 'NONE',  ( 0.7071067811865487940, 0.7071067811865463515, 0.000000000000000000 ) ) ;
#137785=CARTESIAN_POINT ( 'NONE',  ( 34.92499999999998295, -21.72500000000000142, 5.000000000000000000 ) ) ;
#137786=DIRECTION ( 'NONE',  ( 0.7071067811865486830, -0.7071067811865464625, -0.000000000000000000 ) ) ;
#137787=DIRECTION ( 'NONE',  ( -0.7071067811865486830, -0.7071067811865464625, -0.000000000000000000 ) ) ;
#137788=EDGE_CURVE ( 'NONE', #17208, #84616, #133009, .T. ) ;
#137789=EDGE_LOOP ( 'NONE', ( #26956, #70939, #68636, #21046 ) ) ;
#137790=ORIENTED_EDGE ( 'NONE', *, *, #124686, .F. ) ;
#137792=ORIENTED_EDGE ( 'NONE', *, *, #84800, .F. ) ;
#137793=DIRECTION ( 'NONE',  ( 1.000000000000000000, 0.000000000000000000, 0.000000000000000000 ) ) ;
#137794=ORIENTED_EDGE ( 'NONE', *, *, #113326, .F. ) ;
#137795=ORIENTED_EDGE ( 'NONE', *, *, #50463, .F. ) ;
#137796=LINE ( 'NONE', #38471, #127799 ) ;
#137797=CARTESIAN_POINT ( 'NONE',  ( -29.99999999999979394, -4.447814304570784749, 5.000000000000000000 ) ) ;
#137798=ADVANCED_FACE ( 'NONE', ( #102986 ), #81980, .F. ) ;
#137799=ADVANCED_FACE ( 'NONE', ( #80535 ), #38445, .F. ) ;
#137801=VERTEX_POINT ( 'NONE', #35622 ) ;
#137802=DIRECTION ( 'NONE',  ( 0.7071067811865487940, -0.7071067811865463515, 0.000000000000000000 ) ) ;
#137803=ORIENTED_EDGE ( 'NONE', *, *, #138310, .T. ) ;
#137804=ADVANCED_FACE ( 'NONE', ( #79852 ), #126850, .F. ) ;
#137805=DIRECTION ( 'NONE',  ( 0.6830127018922181881, 0.6830127018922202975, -0.2588190451025214056 ) ) ;
#137806=AXIS2_PLACEMENT_3D ( 'NONE', #28769, #117166, #73015 ) ;
#137809=VERTEX_POINT ( 'NONE', #3622 ) ;
#137811=LINE ( 'NONE', #39200, #89295 ) ;
#137813=VECTOR ( 'NONE', #61069, 999.9999999999998863 ) ;
#137814=FACE_OUTER_BOUND ( 'NONE', #56738, .T. ) ;
#137815=ORIENTED_EDGE ( 'NONE', *, *, #44222, .T. ) ;
#137816=ORIENTED_EDGE ( 'NONE', *, *, #120380, .F. ) ;
#137817=DIRECTION ( 'NONE',  ( -0.000000000000000000, 0.000000000000000000, 1.000000000000000000 ) ) ;
#137818=ORIENTED_EDGE ( 'NONE', *, *, #59614, .T. ) ;
#137820=FACE_OUTER_BOUND ( 'NONE', #25711, .T. ) ;
#137821=CARTESIAN_POINT ( 'NONE',  ( -11.81601139373100651, 28.73617430169779041, 5.000000000000000000 ) ) ;
#137824=LINE ( 'NONE', #125516, #76019 ) ;
#137825=AXIS2_PLACEMENT_3D ( 'NONE', #103737, #50825, #5848 ) ;
#137826=LINE ( 'NONE', #126224, #85834 ) ;
#137828=EDGE_CURVE ( 'NONE', #65645, #30899, #24697, .T. ) ;
#137829=ORIENTED_EDGE ( 'NONE', *, *, #50333, .T. ) ;
#137830=FACE_OUTER_BOUND ( 'NONE', #47952, .T. ) ;
#137831=CARTESIAN_POINT ( 'NONE',  ( -26.99999999999980460, -13.06887692260767686, 4.000000000000000000 ) ) ;
#137832=EDGE_LOOP ( 'NONE', ( #138165, #33317, #106906, #80376 ) ) ;
#137833=DIRECTION ( 'NONE',  ( 0.7071067811865486830, -0.7071067811865463515, 0.000000000000000000 ) ) ;
#137834=VERTEX_POINT ( 'NONE', #47919 ) ;
#137835=ORIENTED_EDGE ( 'NONE', *, *, #125672, .T. ) ;
#137838=ORIENTED_EDGE ( 'NONE', *, *, #139058, .T. ) ;
#137841=EDGE_CURVE ( 'NONE', #5588, #1674, #92084, .T. ) ;
#137842=VECTOR ( 'NONE', #88319, 999.9999999999998863 ) ;
#137844=VECTOR ( 'NONE', #88864, 1000.000000000000000 ) ;
#137846=ORIENTED_EDGE ( 'NONE', *, *, #90310, .T. ) ;
#137848=CARTESIAN_POINT ( 'NONE',  ( 18.48921356237309510, -27.52281430457068367, 5.000000000000000000 ) ) ;
#137849=DIRECTION ( 'NONE',  ( 0.7071067811865486830, -0.7071067811865464625, -0.000000000000000000 ) ) ;
#137850=EDGE_CURVE ( 'NONE', #84275, #22022, #92807, .T. ) ;
#137852=CARTESIAN_POINT ( 'NONE',  ( -34.92500000000001137, -4.487538124160448838, 4.000000000000000000 ) ) ;
#137853=DIRECTION ( 'NONE',  ( -0.7071067811865486830, -0.7071067811865464625, -0.000000000000000000 ) ) ;
#137854=DIRECTION ( 'NONE',  ( 0.7071067811865486830, -0.7071067811865464625, -0.000000000000000000 ) ) ;
#137856=CARTESIAN_POINT ( 'NONE',  ( -34.49999999999975842, 4.464255608400450548, 4.994342998332166772 ) ) ;
#137857=DIRECTION ( 'NONE',  ( 0.6830127018922181881, 0.6830127018922202975, -0.2588190451025214056 ) ) ;
#137859=ORIENTED_EDGE ( 'NONE', *, *, #17761, .T. ) ;
#137860=ORIENTED_EDGE ( 'NONE', *, *, #78620, .T. ) ;
#137862=VERTEX_POINT ( 'NONE', #135618 ) ;
#137863=ORIENTED_EDGE ( 'NONE', *, *, #73594, .F. ) ;
#137864=EDGE_CURVE ( 'NONE', #43048, #130061, #49352, .T. ) ;
#137865=EDGE_LOOP ( 'NONE', ( #37751, #96434, #108921, #86463 ) ) ;
#137866=LINE ( 'NONE', #16775, #54898 ) ;
#137867=CARTESIAN_POINT ( 'NONE',  ( -15.29974487139158867, -27.71228299555216879, 4.000000000000000000 ) ) ;
#137868=ORIENTED_EDGE ( 'NONE', *, *, #100328, .T. ) ;
#137869=DIRECTION ( 'NONE',  ( 0.000000000000000000, 1.000000000000000000, 0.000000000000000000 ) ) ;
#137870=FACE_OUTER_BOUND ( 'NONE', #2563, .T. ) ;
#137874=EDGE_CURVE ( 'NONE', #73824, #71954, #103658, .T. ) ;
#137875=ORIENTED_EDGE ( 'NONE', *, *, #143232, .F. ) ;
#137876=CARTESIAN_POINT ( 'NONE',  ( -25.00442415654155681, 3.591886032380943838, 4.000000000000000000 ) ) ;
#137877=CARTESIAN_POINT ( 'NONE',  ( -21.18398860626899349, 28.73617430169802134, 5.000000000000000000 ) ) ;
#137878=CARTESIAN_POINT ( 'NONE',  ( -23.99999999999984013, 12.25461709320618553, -10.07315571508702767 ) ) ;
#137880=LINE ( 'NONE', #38552, #130888 ) ;
#137883=LINE ( 'NONE', #94351, #88483 ) ;
#137884=CARTESIAN_POINT ( 'NONE',  ( 31.78501580275790772, -3.740707523384241728, 15.76143240460131700 ) ) ;
#137885=ORIENTED_EDGE ( 'NONE', *, *, #124940, .T. ) ;
#137886=ORIENTED_EDGE ( 'NONE', *, *, #98152, .T. ) ;
#137888=ORIENTED_EDGE ( 'NONE', *, *, #104489, .T. ) ;
#137889=DIRECTION ( 'NONE',  ( 0.7071067811865487940, -0.7071067811865463515, 0.000000000000000000 ) ) ;
#137890=DIRECTION ( 'NONE',  ( -0.7071067811865487940, 0.7071067811865463515, -0.000000000000000000 ) ) ;
#137892=DIRECTION ( 'NONE',  ( -0.7071067811865487940, 0.7071067811865463515, -0.000000000000000000 ) ) ;
#137895=CARTESIAN_POINT ( 'NONE',  ( 7.499999999999954703, -17.94781430457064531, 5.000000000000000000 ) ) ;
#137898=ORIENTED_EDGE ( 'NONE', *, *, #93771, .F. ) ;
#137899=DIRECTION ( 'NONE',  ( 0.7071067811865487940, 0.7071067811865463515, 0.000000000000000000 ) ) ;
#137900=ORIENTED_EDGE ( 'NONE', *, *, #119514, .F. ) ;
#137901=DIRECTION ( 'NONE',  ( 0.7071067811865486830, -0.7071067811865464625, -0.000000000000000000 ) ) ;
#137902=CARTESIAN_POINT ( 'NONE',  ( 2.207106781186525701, 12.75929247661558996, 5.000000000000000000 ) ) ;
#137903=CARTESIAN_POINT ( 'NONE',  ( 24.96654721599509941, 3.964575861396866685, 4.000000000000000000 ) ) ;
#137904=DIRECTION ( 'NONE',  ( 0.7071067811865487940, 0.7071067811865463515, 0.000000000000000000 ) ) ;
#137909=LINE ( 'NONE', #38583, #33202 ) ;
#137910=EDGE_CURVE ( 'NONE', #80031, #104227, #104392, .T. ) ;
#137911=LINE ( 'NONE', #17526, #115639 ) ;
#137912=CARTESIAN_POINT ( 'NONE',  ( -30.18398860626900060, 28.73617430169808173, 5.000000000000000000 ) ) ;
#137916=VECTOR ( 'NONE', #10556, 1000.000000000000000 ) ;
#137917=DIRECTION ( 'NONE',  ( -0.000000000000000000, -0.3543493200069152693, 0.9351131265310292928 ) ) ;
#137919=VERTEX_POINT ( 'NONE', #41279 ) ;
#137920=ORIENTED_EDGE ( 'NONE', *, *, #106209, .F. ) ;
#137921=LINE ( 'NONE', #37165, #60901 ) ;
#137922=ORIENTED_EDGE ( 'NONE', *, *, #12879, .T. ) ;
#137923=EDGE_CURVE ( 'NONE', #2809, #64090, #19534, .T. ) ;
#137924=CARTESIAN_POINT ( 'NONE',  ( -5.994519915287488843, 28.92564299267942118, 4.000000000000000000 ) ) ;
#137925=ORIENTED_EDGE ( 'NONE', *, *, #122522, .F. ) ;
#137926=LINE ( 'NONE', #71974, #92246 ) ;
#137927=DIRECTION ( 'NONE',  ( -0.7071067811865486830, -0.7071067811865464625, 0.000000000000000000 ) ) ;
#137928=CARTESIAN_POINT ( 'NONE',  ( -14.20710678118645376, 12.75929247661558996, 5.000000000000000000 ) ) ;
#137929=FACE_BOUND ( 'NONE', #5651, .T. ) ;
#137930=LINE ( 'NONE', #5934, #38757 ) ;
#137932=CARTESIAN_POINT ( 'NONE',  ( 8.999999999999934275, -13.06887692260767686, 4.000000000000000000 ) ) ;
#137933=ORIENTED_EDGE ( 'NONE', *, *, #51248, .F. ) ;
#137937=ORIENTED_EDGE ( 'NONE', *, *, #115290, .F. ) ;
#137938=CARTESIAN_POINT ( 'NONE',  ( 22.49999999999984368, -20.56887692260760048, 4.000000000000000000 ) ) ;
#137939=AXIS2_PLACEMENT_3D ( 'NONE', #46827, #91014, #55520 ) ;
#137940=ORIENTED_EDGE ( 'NONE', *, *, #80098, .T. ) ;
#137941=EDGE_CURVE ( 'NONE', #53245, #142744, #64473, .T. ) ;
#137942=VECTOR ( 'NONE', #48751, 1000.000000000000227 ) ;
#137943=EDGE_CURVE ( 'NONE', #110128, #42427, #42024, .T. ) ;
#137944=VERTEX_POINT ( 'NONE', #52854 ) ;
#137946=ORIENTED_EDGE ( 'NONE', *, *, #133117, .F. ) ;
#137947=VECTOR ( 'NONE', #14584, 1000.000000000000227 ) ;
#137948=LINE ( 'NONE', #18251, #95071 ) ;
#137950=FACE_OUTER_BOUND ( 'NONE', #34785, .T. ) ;
#137951=ORIENTED_EDGE ( 'NONE', *, *, #32894, .F. ) ;
#137952=VECTOR ( 'NONE', #108365, 1000.000000000000000 ) ;
#137953=EDGE_CURVE ( 'NONE', #85512, #18266, #39159, .T. ) ;
#137954=EDGE_CURVE ( 'NONE', #85156, #8752, #139205, .T. ) ;
#137955=CARTESIAN_POINT ( 'NONE',  ( -34.92500000000001137, -6.791953661863761482, 15.99560845316869795 ) ) ;
#137956=DIRECTION ( 'NONE',  ( 0.7071067811865486830, -0.7071067811865464625, -0.000000000000000000 ) ) ;
#137957=DIRECTION ( 'NONE',  ( 1.000000000000000000, 0.000000000000000000, 0.000000000000000000 ) ) ;
#137959=ORIENTED_EDGE ( 'NONE', *, *, #45813, .T. ) ;
#137962=EDGE_LOOP ( 'NONE', ( #59697, #51806, #25286, #754 ) ) ;
#137963=ORIENTED_EDGE ( 'NONE', *, *, #63060, .T. ) ;
#137964=ORIENTED_EDGE ( 'NONE', *, *, #30964, .T. ) ;
#137965=DIRECTION ( 'NONE',  ( -0.000000000000000000, 0.000000000000000000, 1.000000000000000000 ) ) ;
#137966=DIRECTION ( 'NONE',  ( 0.6830127018922180770, -0.6830127018922204085, -0.2588190451025213501 ) ) ;
#137967=ADVANCED_FACE ( 'NONE', ( #140588 ), #141311, .F. ) ;
#137968=EDGE_CURVE ( 'NONE', #41375, #108415, #116710, .T. ) ;
#137969=CARTESIAN_POINT ( 'NONE',  ( -5.999999999999952927, -21.41253812416053748, 4.000000000000000000 ) ) ;
#137970=ORIENTED_EDGE ( 'NONE', *, *, #40069, .F. ) ;
#137971=LINE ( 'NONE', #81468, #94895 ) ;
#137972=EDGE_CURVE ( 'NONE', #122347, #114208, #30422, .T. ) ;
#137973=PLANE ( 'NONE',  #4958 ) ;
#137975=CARTESIAN_POINT ( 'NONE',  ( 12.00548008471251293, 28.92564299267929684, 4.000000000000000000 ) ) ;
#137976=ORIENTED_EDGE ( 'NONE', *, *, #22790, .F. ) ;
#137977=CARTESIAN_POINT ( 'NONE',  ( 6.524001385854438340, 22.03583458319437582, 4.979811245910090278 ) ) ;
#137978=LINE ( 'NONE', #40803, #21163 ) ;
#137979=LINE ( 'NONE', #50258, #135468 ) ;
#137980=EDGE_CURVE ( 'NONE', #63953, #54435, #117392, .T. ) ;
#137981=DIRECTION ( 'NONE',  ( -0.7071067811865487940, 0.7071067811865463515, 0.000000000000000000 ) ) ;
#137982=VERTEX_POINT ( 'NONE', #18809 ) ;
#137983=PLANE ( 'NONE',  #102622 ) ;
#137984=ORIENTED_EDGE ( 'NONE', *, *, #142821, .T. ) ;
#137985=CARTESIAN_POINT ( 'NONE',  ( 26.99999999999981526, 13.93112307739204603, 4.000000000000000000 ) ) ;
#137986=DIRECTION ( 'NONE',  ( -0.7071067811865486830, -0.7071067811865464625, 0.000000000000000000 ) ) ;
#137987=LINE ( 'NONE', #116930, #33239 ) ;
#137988=ORIENTED_EDGE ( 'NONE', *, *, #7381, .T. ) ;
#137989=DIRECTION ( 'NONE',  ( -0.7071067811865486830, -0.7071067811865464625, 0.000000000000000000 ) ) ;
#137990=CARTESIAN_POINT ( 'NONE',  ( 14.99999999999989519, -19.06887692260762179, 4.000000000000000000 ) ) ;
#137991=FACE_OUTER_BOUND ( 'NONE', #43604, .T. ) ;
#137993=EDGE_LOOP ( 'NONE', ( #81440, #74902, #122338, #32669 ) ) ;
#137994=CARTESIAN_POINT ( 'NONE',  ( -34.92500000000001137, -14.14387692260741325, 4.000000000000000000 ) ) ;
#137999=EDGE_CURVE ( 'NONE', #29164, #113129, #74657, .T. ) ;
#138000=VERTEX_POINT ( 'NONE', #28285 ) ;
#138001=LINE ( 'NONE', #3858, #125933 ) ;
#138002=DIRECTION ( 'NONE',  ( -0.7071067811865486830, -0.7071067811865464625, 0.000000000000000000 ) ) ;
#138003=EDGE_CURVE ( 'NONE', #41816, #18858, #105800, .T. ) ;
#138005=VECTOR ( 'NONE', #129504, 1000.000000000000000 ) ;
#138006=LINE ( 'NONE', #16933, #59828 ) ;
#138007=LINE ( 'NONE', #92326, #25293 ) ;
#138008=CARTESIAN_POINT ( 'NONE',  ( -17.99999999999987210, 13.93112307739204070, 4.000000000000000000 ) ) ;
#138009=FACE_OUTER_BOUND ( 'NONE', #64604, .T. ) ;
#138010=AXIS2_PLACEMENT_3D ( 'NONE', #78531, #56816, #1635 ) ;
#138011=ORIENTED_EDGE ( 'NONE', *, *, #101956, .F. ) ;
#138012=DIRECTION ( 'NONE',  ( -0.7071067811865486830, -0.7071067811865464625, 0.000000000000000000 ) ) ;
#138013=LINE ( 'NONE', #39424, #26147 ) ;
#138014=DIRECTION ( 'NONE',  ( -0.000000000000000000, 0.000000000000000000, 1.000000000000000000 ) ) ;
#138016=CARTESIAN_POINT ( 'NONE',  ( -0.7700427945779352301, 21.73644205237998150, 5.000000000000000888 ) ) ;
#138017=VERTEX_POINT ( 'NONE', #18065 ) ;
#138019=ORIENTED_EDGE ( 'NONE', *, *, #132337, .T. ) ;
#138020=VECTOR ( 'NONE', #79417, 1000.000000000000227 ) ;
#138021=VERTEX_POINT ( 'NONE', #118100 ) ;
#138022=DIRECTION ( 'NONE',  ( -0.3543493200069162685, -0.000000000000000000, -0.9351131265310288487 ) ) ;
#138023=DIRECTION ( 'NONE',  ( -0.3543493200069162685, -0.000000000000000000, -0.9351131265310288487 ) ) ;
#138025=PLANE ( 'NONE',  #46419 ) ;
#138027=CARTESIAN_POINT ( 'NONE',  ( 19.05000000000000071, 3.174999999999997158, 4.000000000000000000 ) ) ;
#138030=ORIENTED_EDGE ( 'NONE', *, *, #140707, .T. ) ;
#138031=DIRECTION ( 'NONE',  ( 0.6830127018922181881, 0.6830127018922202975, -0.2588190451025214056 ) ) ;
#138032=CARTESIAN_POINT ( 'NONE',  ( 13.49999999999991473, 7.087461875839172087, 4.000000000000000000 ) ) ;
#138033=DIRECTION ( 'NONE',  ( -0.7071067811865486830, -0.7071067811865464625, 0.000000000000000000 ) ) ;
#138034=LINE ( 'NONE', #13367, #59003 ) ;
#138035=VECTOR ( 'NONE', #36445, 1000.000000000000000 ) ;
#138036=CARTESIAN_POINT ( 'NONE',  ( 33.70710678118631165, -9.740707523384182664, 5.000000000000000000 ) ) ;
#138039=CARTESIAN_POINT ( 'NONE',  ( -34.92500000000001137, -22.22500000000000142, 4.500000000000000888 ) ) ;
#138040=VERTEX_POINT ( 'NONE', #118845 ) ;
#138041=EDGE_LOOP ( 'NONE', ( #4783, #99587, #114088, #67408 ) ) ;
#138043=CARTESIAN_POINT ( 'NONE',  ( -54.48921356237310221, -27.52281430457093236, 5.000000000000000000 ) ) ;
#138044=AXIS2_PLACEMENT_3D ( 'NONE', #95778, #40014, #139325 ) ;
#138045=DIRECTION ( 'NONE',  ( 0.6830127018922181881, 0.6830127018922202975, -0.2588190451025214056 ) ) ;
#138047=EDGE_CURVE ( 'NONE', #31906, #65260, #7196, .T. ) ;
#138048=AXIS2_PLACEMENT_3D ( 'NONE', #80618, #3026, #13882 ) ;
#138049=ORIENTED_EDGE ( 'NONE', *, *, #47032, .T. ) ;
#138050=CARTESIAN_POINT ( 'NONE',  ( 24.70710678118637915, 17.25929247661554555, 5.000000000000000000 ) ) ;
#138051=CARTESIAN_POINT ( 'NONE',  ( 22.49999999999984723, 16.77039438581781639, 0.4657186855307219875 ) ) ;
#138053=DIRECTION ( 'NONE',  ( -0.000000000000000000, 0.000000000000000000, 1.000000000000000000 ) ) ;
#138055=ORIENTED_EDGE ( 'NONE', *, *, #70984, .F. ) ;
#138056=FACE_OUTER_BOUND ( 'NONE', #25116, .T. ) ;
#138057=CARTESIAN_POINT ( 'NONE',  ( -26.29289321881326558, 2.259292476615690770, 5.000000000000000000 ) ) ;
#138058=DIRECTION ( 'NONE',  ( -0.7071067811865486830, -0.7071067811865464625, 0.000000000000000000 ) ) ;
#138060=EDGE_CURVE ( 'NONE', #45656, #121222, #139917, .T. ) ;
#138061=LINE ( 'NONE', #106103, #136782 ) ;
#138062=DIRECTION ( 'NONE',  ( -0.7071067811865487940, 0.7071067811865463515, 0.000000000000000000 ) ) ;
#138063=VERTEX_POINT ( 'NONE', #96345 ) ;
#138064=EDGE_CURVE ( 'NONE', #35117, #91654, #63779, .T. ) ;
#138065=CARTESIAN_POINT ( 'NONE',  ( 81.48921356237309510, -27.52281430457112066, 5.000000000000000000 ) ) ;
#138068=DIRECTION ( 'NONE',  ( -0.7071067811865486830, -0.7071067811865464625, 0.000000000000000000 ) ) ;
#138071=EDGE_CURVE ( 'NONE', #115946, #99168, #134022, .T. ) ;
#138072=PLANE ( 'NONE',  #91550 ) ;
#138073=PLANE ( 'NONE',  #20931 ) ;
#138074=CARTESIAN_POINT ( 'NONE',  ( 28.88982677111768638, -22.22500000000000142, 4.785647885939353863 ) ) ;
#138076=DIRECTION ( 'NONE',  ( 1.000000000000000000, 0.000000000000000000, 0.000000000000000000 ) ) ;
#138077=ORIENTED_EDGE ( 'NONE', *, *, #93148, .F. ) ;
#138078=ORIENTED_EDGE ( 'NONE', *, *, #107993, .T. ) ;
#138079=VECTOR ( 'NONE', #80296, 1000.000000000000000 ) ;
#138081=VERTEX_POINT ( 'NONE', #78948 ) ;
#138082=EDGE_CURVE ( 'NONE', #871, #43439, #21685, .T. ) ;
#138084=ORIENTED_EDGE ( 'NONE', *, *, #76517, .T. ) ;
#138085=CARTESIAN_POINT ( 'NONE',  ( -68.99451991528748351, 28.92564299267986172, 4.000000000000000000 ) ) ;
#138086=ORIENTED_EDGE ( 'NONE', *, *, #33594, .T. ) ;
#138088=CARTESIAN_POINT ( 'NONE',  ( 24.79289321881329045, -5.240707523384227073, 5.000000000000000000 ) ) ;
#138089=AXIS2_PLACEMENT_3D ( 'NONE', #119270, #42477, #8345 ) ;
#138090=EDGE_CURVE ( 'NONE', #37148, #38733, #110098, .T. ) ;
#138091=EDGE_CURVE ( 'NONE', #72213, #33945, #123157, .T. ) ;
#138092=( BOUNDED_CURVE ( )  B_SPLINE_CURVE ( 3, ( #139833, #27442, #116616, #140499 ),
 .UNSPECIFIED., .F., .T. ) 
 B_SPLINE_CURVE_WITH_KNOTS ( ( 4, 4 ),
 ( 5.920967161967927161, 7.341195215986571654 ),
 .UNSPECIFIED. ) 
 CURVE ( )  GEOMETRIC_REPRESENTATION_ITEM ( )  RATIONAL_B_SPLINE_CURVE ( ( 1.000000000000000000, 0.8388583629366757055, 0.8388583629366757055, 1.000000000000000000 ) ) 
 REPRESENTATION_ITEM ( '' )  );
#138093=FACE_BOUND ( 'NONE', #125660, .T. ) ;
#138095=LINE ( 'NONE', #72888, #111497 ) ;
#138096=LINE ( 'NONE', #38084, #126821 ) ;
#138097=ORIENTED_EDGE ( 'NONE', *, *, #126915, .T. ) ;
#138098=LINE ( 'NONE', #48963, #46412 ) ;
#138100=VECTOR ( 'NONE', #53988, 999.9999999999998863 ) ;
#138101=VERTEX_POINT ( 'NONE', #31843 ) ;
#138102=ORIENTED_EDGE ( 'NONE', *, *, #137048, .T. ) ;
#138104=VERTEX_POINT ( 'NONE', #110797 ) ;
#138105=LINE ( 'NONE', #95302, #53584 ) ;
#138106=EDGE_CURVE ( 'NONE', #95146, #107914, #20951, .T. ) ;
#138108=CARTESIAN_POINT ( 'NONE',  ( -18.18398860626898994, 28.73617430169800002, 5.000000000000000000 ) ) ;
#138109=EDGE_CURVE ( 'NONE', #71394, #23245, #76810, .T. ) ;
#138110=EDGE_CURVE ( 'NONE', #81346, #101337, #108648, .T. ) ;
#138111=DIRECTION ( 'NONE',  ( -0.000000000000000000, -0.3543493200069152693, 0.9351131265310292928 ) ) ;
#138112=ORIENTED_EDGE ( 'NONE', *, *, #123921, .F. ) ;
#138113=PLANE ( 'NONE',  #92343 ) ;
#138114=DIRECTION ( 'NONE',  ( -0.000000000000000000, 0.000000000000000000, 1.000000000000000000 ) ) ;
#138116=CARTESIAN_POINT ( 'NONE',  ( -29.99999999999978684, -11.35517001088074274, -1.126524801160180056 ) ) ;
#138117=PLANE ( 'NONE',  #143119 ) ;
#138119=CARTESIAN_POINT ( 'NONE',  ( 0.000000000000000000, 0.000000000000000000, 5.000000000000000000 ) ) ;
#138120=FACE_OUTER_BOUND ( 'NONE', #106760, .T. ) ;
#138121=DIRECTION ( 'NONE',  ( -0.000000000000000000, -0.3543493200069152693, 0.9351131265310292928 ) ) ;
#138122=ORIENTED_EDGE ( 'NONE', *, *, #124268, .T. ) ;
#138123=ADVANCED_FACE ( 'NONE', ( #120233 ), #97809, .F. ) ;
#138124=CARTESIAN_POINT ( 'NONE',  ( -6.707106781186496391, -0.7407075233842753681, 5.000000000000000000 ) ) ;
#138125=LINE ( 'NONE', #58482, #83578 ) ;
#138128=ORIENTED_EDGE ( 'NONE', *, *, #53000, .F. ) ;
#138129=EDGE_CURVE ( 'NONE', #8853, #51846, #99208, .T. ) ;
#138130=ADVANCED_FACE ( 'NONE', ( #33318 ), #77520, .F. ) ;
#138131=ORIENTED_EDGE ( 'NONE', *, *, #71448, .F. ) ;
#138133=ORIENTED_EDGE ( 'NONE', *, *, #70898, .F. ) ;
#138134=VECTOR ( 'NONE', #31290, 1000.000000000000000 ) ;
#138135=VECTOR ( 'NONE', #5026, 1000.000000000000227 ) ;
#138136=VECTOR ( 'NONE', #176, 999.9999999999998863 ) ;
#138137=EDGE_CURVE ( 'NONE', #73159, #949, #132624, .T. ) ;
#138140=ADVANCED_FACE ( 'NONE', ( #65217 ), #1329, .F. ) ;
#138141=ORIENTED_EDGE ( 'NONE', *, *, #64686, .F. ) ;
#138143=ORIENTED_EDGE ( 'NONE', *, *, #43504, .F. ) ;
#138144=CARTESIAN_POINT ( 'NONE',  ( -53.99451991528749062, 28.92564299267975869, 4.000000000000000000 ) ) ;
#138145=VECTOR ( 'NONE', #100600, 1000.000000000000114 ) ;
#138146=DIRECTION ( 'NONE',  ( -0.7071067811865486830, -0.7071067811865464625, 0.000000000000000000 ) ) ;
#138147=EDGE_CURVE ( 'NONE', #31910, #80563, #66626, .T. ) ;
#138148=DIRECTION ( 'NONE',  ( -0.000000000000000000, 0.3543493200069153248, 0.9351131265310292928 ) ) ;
#138149=ORIENTED_EDGE ( 'NONE', *, *, #50685, .T. ) ;
#138150=ORIENTED_EDGE ( 'NONE', *, *, #48087, .T. ) ;
#138151=DIRECTION ( 'NONE',  ( -0.6830127018922180770, -0.6830127018922204085, -0.2588190451025213501 ) ) ;
#138153=DIRECTION ( 'NONE',  ( 0.7071067811865487940, -0.7071067811865463515, 0.000000000000000000 ) ) ;
#138154=ORIENTED_EDGE ( 'NONE', *, *, #122223, .T. ) ;
#138155=DIRECTION ( 'NONE',  ( -0.7071067811865487940, 0.7071067811865463515, -0.000000000000000000 ) ) ;
#138156=ORIENTED_EDGE ( 'NONE', *, *, #44201, .F. ) ;
#138157=VERTEX_POINT ( 'NONE', #86944 ) ;
#138158=ORIENTED_EDGE ( 'NONE', *, *, #19765, .F. ) ;
#138159=VERTEX_POINT ( 'NONE', #99959 ) ;
#138160=CARTESIAN_POINT ( 'NONE',  ( -34.92500000000001137, 21.72500000000000142, 5.000000000000000000 ) ) ;
#138161=EDGE_CURVE ( 'NONE', #9514, #116559, #44917, .T. ) ;
#138162=DIRECTION ( 'NONE',  ( 1.000000000000000000, 0.000000000000000000, 0.000000000000000000 ) ) ;
#138163=CARTESIAN_POINT ( 'NONE',  ( -57.18398860626899705, 28.73617430169827358, 5.000000000000000000 ) ) ;
#138164=CARTESIAN_POINT ( 'NONE',  ( -44.99451991528749772, 28.92564299267969474, 4.000000000000000000 ) ) ;
#138165=ORIENTED_EDGE ( 'NONE', *, *, #23138, .F. ) ;
#138166=ORIENTED_EDGE ( 'NONE', *, *, #120742, .F. ) ;
#138167=CARTESIAN_POINT ( 'NONE',  ( -17.70025512860841488, -27.71228299555193786, 4.000000000000000000 ) ) ;
#138168=ADVANCED_FACE ( 'NONE', ( #54346 ), #122404, .F. ) ;
#138169=EDGE_CURVE ( 'NONE', #7759, #61677, #33997, .T. ) ;
#138170=DIRECTION ( 'NONE',  ( -0.000000000000000000, 0.000000000000000000, 1.000000000000000000 ) ) ;
#138171=DIRECTION ( 'NONE',  ( -1.000000000000000000, 2.223259271439533943E-14, 0.000000000000000000 ) ) ;
#138172=CARTESIAN_POINT ( 'NONE',  ( -19.21071296386495675, 9.141836041257182188, 4.000000000000000000 ) ) ;
#138174=ORIENTED_EDGE ( 'NONE', *, *, #65932, .F. ) ;
#138176=ORIENTED_EDGE ( 'NONE', *, *, #131926, .T. ) ;
#138177=CARTESIAN_POINT ( 'NONE',  ( 56.99451991528749062, 28.92564299267978001, 4.000000000000000000 ) ) ;
#138179=DIRECTION ( 'NONE',  ( -0.7071067811865486830, -0.7071067811865464625, -0.000000000000000000 ) ) ;
#138180=VECTOR ( 'NONE', #54463, 1000.000000000000000 ) ;
#138182=EDGE_CURVE ( 'NONE', #140758, #38440, #100680, .T. ) ;
#138185=LINE ( 'NONE', #61383, #62611 ) ;
#138187=LINE ( 'NONE', #117125, #52439 ) ;
#138188=CARTESIAN_POINT ( 'NONE',  ( 22.35824297541125816, 15.75929247661555088, 19.34181609438694238 ) ) ;
#138189=LINE ( 'NONE', #48316, #20964 ) ;
#138190=CIRCLE ( 'NONE', #75695, 5.968999999999998529 ) ;
#138191=ORIENTED_EDGE ( 'NONE', *, *, #39267, .T. ) ;
#138192=CARTESIAN_POINT ( 'NONE',  ( -42.48921356237308800, -27.52281430457085065, 5.000000000000000000 ) ) ;
#138193=ORIENTED_EDGE ( 'NONE', *, *, #71336, .T. ) ;
#138194=CARTESIAN_POINT ( 'NONE',  ( -60.29974487139158867, -27.71228299555248142, 4.000000000000000000 ) ) ;
#138195=DIRECTION ( 'NONE',  ( -0.000000000000000000, 0.3543493200069153248, 0.9351131265310292928 ) ) ;
#138196=EDGE_LOOP ( 'NONE', ( #39991, #89351, #36307, #95564 ) ) ;
#138198=DIRECTION ( 'NONE',  ( -0.7071067811865486830, -0.7071067811865464625, -0.000000000000000000 ) ) ;
#138199=CARTESIAN_POINT ( 'NONE',  ( -69.48921356237309510, -27.52281430457103895, 5.000000000000000000 ) ) ;
#138200=ORIENTED_EDGE ( 'NONE', *, *, #121138, .F. ) ;
#138201=ORIENTED_EDGE ( 'NONE', *, *, #114239, .T. ) ;
#138202=CARTESIAN_POINT ( 'NONE',  ( 34.92499999999998295, -22.22500000000000142, 4.500000000000000888 ) ) ;
#138203=VERTEX_POINT ( 'NONE', #114394 ) ;
#138204=LINE ( 'NONE', #26582, #126317 ) ;
#138205=VECTOR ( 'NONE', #65405, 1000.000000000000000 ) ;
#138207=FACE_OUTER_BOUND ( 'NONE', #130711, .T. ) ;
#138209=ORIENTED_EDGE ( 'NONE', *, *, #91129, .T. ) ;
#138210=VECTOR ( 'NONE', #63424, 1000.000000000000227 ) ;
#138211=CARTESIAN_POINT ( 'NONE',  ( -15.79289321881334551, -20.24070752338407431, 5.000000000000000000 ) ) ;
#138212=ADVANCED_FACE ( 'NONE', ( #15064 ), #70235, .F. ) ;
#138213=CARTESIAN_POINT ( 'NONE',  ( 20.99999999999985079, -21.41253812416053748, 4.000000000000000000 ) ) ;
#138216=CARTESIAN_POINT ( 'NONE',  ( -33.18398860626899705, 28.73617430169810305, 5.000000000000000000 ) ) ;
#138217=ORIENTED_EDGE ( 'NONE', *, *, #21651, .T. ) ;
#138218=LINE ( 'NONE', #7681, #141739 ) ;
#138219=VERTEX_POINT ( 'NONE', #25968 ) ;
#138221=LINE ( 'NONE', #4789, #121805 ) ;
#138222=CARTESIAN_POINT ( 'NONE',  ( 69.18398860626899705, 28.73617430169835529, 5.000000000000000000 ) ) ;
#138223=CARTESIAN_POINT ( 'NONE',  ( -15.32816939922342492, -3.740707523384241728, 4.000000000000000000 ) ) ;
#138224=ORIENTED_EDGE ( 'NONE', *, *, #65542, .T. ) ;
#138226=EDGE_CURVE ( 'NONE', #6909, #90219, #91251, .T. ) ;
#138227=LINE ( 'NONE', #125211, #18776 ) ;
#138231=DIRECTION ( 'NONE',  ( 0.7071067811865487940, 0.7071067811865463515, -0.000000000000000000 ) ) ;
#138232=DIRECTION ( 'NONE',  ( 0.7071067811865487940, 0.7071067811865463515, 0.000000000000000000 ) ) ;
#138233=VERTEX_POINT ( 'NONE', #82494 ) ;
#138234=DIRECTION ( 'NONE',  ( 0.7071067811865487940, 0.7071067811865463515, -0.000000000000000000 ) ) ;
#138235=CARTESIAN_POINT ( 'NONE',  ( -34.42500000000000426, 10.54139925780190801, 5.000000000000000000 ) ) ;
#138237=AXIS2_PLACEMENT_3D ( 'NONE', #47559, #90282, #44704 ) ;
#138238=LINE ( 'NONE', #51954, #109464 ) ;
#138240=EDGE_CURVE ( 'NONE', #92832, #117294, #81078, .T. ) ;
#138241=EDGE_CURVE ( 'NONE', #97535, #140583, #103497, .T. ) ;
#138242=VERTEX_POINT ( 'NONE', #47756 ) ;
#138243=VERTEX_POINT ( 'NONE', #48428 ) ;
#138246=ADVANCED_FACE ( 'NONE', ( #36144 ), #68091, .T. ) ;
#138248=AXIS2_PLACEMENT_3D ( 'NONE', #101980, #122277, #66510 ) ;
#138249=FACE_OUTER_BOUND ( 'NONE', #11764, .T. ) ;
#138250=VECTOR ( 'NONE', #127737, 1000.000000000000000 ) ;
#138253=CARTESIAN_POINT ( 'NONE',  ( 0.000000000000000000, 0.000000000000000000, 5.000000000000000000 ) ) ;
#138254=CARTESIAN_POINT ( 'NONE',  ( -32.29289321881321939, -0.7407075233842753681, 5.000000000000000000 ) ) ;
#138255=EDGE_CURVE ( 'NONE', #76898, #33831, #4870, .T. ) ;
#138256=ORIENTED_EDGE ( 'NONE', *, *, #121909, .T. ) ;
#138257=PLANE ( 'NONE',  #46710 ) ;
#138259=FACE_OUTER_BOUND ( 'NONE', #98916, .T. ) ;
#138260=EDGE_CURVE ( 'NONE', #112045, #78508, #57917, .T. ) ;
#138261=ORIENTED_EDGE ( 'NONE', *, *, #23410, .F. ) ;
#138262=VERTEX_POINT ( 'NONE', #37570 ) ;
#138263=CARTESIAN_POINT ( 'NONE',  ( 30.18398860626900060, 28.73617430169808173, 5.000000000000000000 ) ) ;
#138265=DIRECTION ( 'NONE',  ( -0.6830127018922181881, 0.6830127018922202975, -0.2588190451025214056 ) ) ;
#138267=CARTESIAN_POINT ( 'NONE',  ( -2.206660635421508143, 21.75929247661549937, 4.998822639870708073 ) ) ;
#138268=AXIS2_PLACEMENT_3D ( 'NONE', #22557, #79880, #103014 ) ;
#138269=EDGE_CURVE ( 'NONE', #14195, #10130, #47070, .T. ) ;
#138271=( BOUNDED_CURVE ( )  B_SPLINE_CURVE ( 3, ( #57558, #13285, #101748, #124217 ),
 .UNSPECIFIED., .F., .T. ) 
 B_SPLINE_CURVE_WITH_KNOTS ( ( 4, 4 ),
 ( 2.228251278275057867, 2.286295730127291037 ),
 .UNSPECIFIED. ) 
 CURVE ( )  GEOMETRIC_REPRESENTATION_ITEM ( )  RATIONAL_B_SPLINE_CURVE ( ( 1.000000000000000000, 0.9997192565072046122, 0.9997192565072046122, 1.000000000000000000 ) ) 
 REPRESENTATION_ITEM ( '' )  );
#138272=CARTESIAN_POINT ( 'NONE',  ( 26.99999999999980815, 4.931123077392136622, 4.000000000000000000 ) ) ;
#138274=ORIENTED_EDGE ( 'NONE', *, *, #141008, .F. ) ;
#138275=VECTOR ( 'NONE', #62932, 1000.000000000000000 ) ;
#138276=ORIENTED_EDGE ( 'NONE', *, *, #91531, .F. ) ;
#138278=EDGE_LOOP ( 'NONE', ( #87673, #72713, #72940, #120831 ) ) ;
#138279=ADVANCED_FACE ( 'NONE', ( #26675 ), #101377, .F. ) ;
#138280=VECTOR ( 'NONE', #71570, 999.9999999999998863 ) ;
#138281=DIRECTION ( 'NONE',  ( -0.7071067811865487940, 0.7071067811865463515, -0.000000000000000000 ) ) ;
#138282=EDGE_CURVE ( 'NONE', #67593, #2749, #135460, .T. ) ;
#138284=EDGE_LOOP ( 'NONE', ( #39150, #13888, #72228, #136988 ) ) ;
#138285=CARTESIAN_POINT ( 'NONE',  ( -15.70701326429294475, -21.74070752338406365, 4.999753212805219782 ) ) ;
#138286=CARTESIAN_POINT ( 'NONE',  ( -2.700255128608413990, -27.71228299555204089, 4.000000000000000000 ) ) ;
#138287=EDGE_CURVE ( 'NONE', #19965, #109971, #90518, .T. ) ;
#138288=DIRECTION ( 'NONE',  ( -0.000000000000000000, 0.3543493200069153248, 0.9351131265310292928 ) ) ;
#138289=AXIS2_PLACEMENT_3D ( 'NONE', #8532, #142673, #52781 ) ;
#138291=DIRECTION ( 'NONE',  ( -0.6830127018922181881, 0.6830127018922202975, -0.2588190451025214056 ) ) ;
#138292=ORIENTED_EDGE ( 'NONE', *, *, #64775, .F. ) ;
#138293=ADVANCED_FACE ( 'NONE', ( #35454 ), #134761, .F. ) ;
#138296=ORIENTED_EDGE ( 'NONE', *, *, #70412, .F. ) ;
#138297=CARTESIAN_POINT ( 'NONE',  ( 27.48921356237309155, -27.52281430457074762, 5.000000000000000000 ) ) ;
#138298=VERTEX_POINT ( 'NONE', #79688 ) ;
#138299=EDGE_LOOP ( 'NONE', ( #39224, #121010, #19246, #121333, #53737 ) ) ;
#138301=ORIENTED_EDGE ( 'NONE', *, *, #128798, .F. ) ;
#138302=ORIENTED_EDGE ( 'NONE', *, *, #61151, .T. ) ;
#138304=VERTEX_POINT ( 'NONE', #58658 ) ;
#138305=DIRECTION ( 'NONE',  ( -0.6830127018922181881, 0.6830127018922202975, -0.2588190451025214056 ) ) ;
#138306=CARTESIAN_POINT ( 'NONE',  ( 6.489213562373093325, -27.52281430457059841, 5.000000000000000000 ) ) ;
#138307=VECTOR ( 'NONE', #95111, 1000.000000000000000 ) ;
#138309=FACE_OUTER_BOUND ( 'NONE', #99071, .T. ) ;
#138310=EDGE_CURVE ( 'NONE', #45577, #33663, #102824, .T. ) ;
#138311=CARTESIAN_POINT ( 'NONE',  ( -3.792893218813431222, 6.759292476615651246, 5.000000000000000000 ) ) ;
#138312=FACE_OUTER_BOUND ( 'NONE', #282, .T. ) ;
#138313=EDGE_CURVE ( 'NONE', #122295, #75714, #129162, .T. ) ;
#138314=DIRECTION ( 'NONE',  ( -0.6830127018922181881, 0.6830127018922202975, -0.2588190451025214056 ) ) ;
#138317=ORIENTED_EDGE ( 'NONE', *, *, #116127, .F. ) ;
#138319=LINE ( 'NONE', #5629, #1198 ) ;
#138320=ORIENTED_EDGE ( 'NONE', *, *, #119556, .T. ) ;
#138321=ORIENTED_EDGE ( 'NONE', *, *, #108139, .T. ) ;
#138322=LINE ( 'NONE', #31527, #47350 ) ;
#138323=ORIENTED_EDGE ( 'NONE', *, *, #94915, .T. ) ;
#138325=DIRECTION ( 'NONE',  ( -0.7071067811865486830, 0.7071067811865464625, 0.000000000000000000 ) ) ;
#138326=CARTESIAN_POINT ( 'NONE',  ( 33.18398860626899705, 28.73617430169810305, 5.000000000000000000 ) ) ;
#138327=VECTOR ( 'NONE', #13426, 1000.000000000000000 ) ;
#138328=FACE_OUTER_BOUND ( 'NONE', #20619, .T. ) ;
#138329=FACE_OUTER_BOUND ( 'NONE', #127990, .T. ) ;
#138332=VERTEX_POINT ( 'NONE', #94761 ) ;
#138334=VECTOR ( 'NONE', #2748, 1000.000000000000227 ) ;
#138336=AXIS2_PLACEMENT_3D ( 'NONE', #120187, #109352, #121638 ) ;
#138339=CARTESIAN_POINT ( 'NONE',  ( -48.29974487139158867, -27.71228299555239971, 4.000000000000000000 ) ) ;
#138340=CARTESIAN_POINT ( 'NONE',  ( 30.70701326429282929, -21.74070752338406365, 4.999753212805224223 ) ) ;
#138341=ORIENTED_EDGE ( 'NONE', *, *, #52343, .T. ) ;
#138342=EDGE_LOOP ( 'NONE', ( #108068, #55731, #26700, #136725, #68347, #134086 ) ) ;
#138343=ORIENTED_EDGE ( 'NONE', *, *, #5526, .T. ) ;
#138344=LINE ( 'NONE', #17947, #123700 ) ;
#138345=DIRECTION ( 'NONE',  ( 1.000000000000000000, 0.000000000000000000, 0.000000000000000000 ) ) ;
#138346=VECTOR ( 'NONE', #125954, 1000.000000000000000 ) ;
#138347=CARTESIAN_POINT ( 'NONE',  ( 5.700255128608413102, -27.71228299555201957, 4.000000000000000000 ) ) ;
#138349=ADVANCED_FACE ( 'NONE', ( #129541 ), #27363, .F. ) ;
#138350=CARTESIAN_POINT ( 'NONE',  ( -36.18398860626899705, 28.73617430169812437, 5.000000000000000000 ) ) ;
#138351=FACE_OUTER_BOUND ( 'NONE', #142293, .T. ) ;
#138353=CARTESIAN_POINT ( 'NONE',  ( -6.489213562373093325, -27.52281430457059841, 5.000000000000000000 ) ) ;
#138354=CARTESIAN_POINT ( 'NONE',  ( 0.000000000000000000, 0.000000000000000000, 5.000000000000000000 ) ) ;
#138355=ORIENTED_EDGE ( 'NONE', *, *, #47489, .F. ) ;
#138356=CARTESIAN_POINT ( 'NONE',  ( 28.49999999999980460, 0.4497235411627734103, -5.599840258123474968 ) ) ;
#138357=DIRECTION ( 'NONE',  ( 0.7071067811865487940, 0.7071067811865463515, 0.000000000000000000 ) ) ;
#138358=ORIENTED_EDGE ( 'NONE', *, *, #57775, .F. ) ;
#138359=CARTESIAN_POINT ( 'NONE',  ( -18.32816939922339472, -12.74070752338414891, 4.000000000000000000 ) ) ;
#138361=EDGE_LOOP ( 'NONE', ( #135666, #47944, #128768, #55349 ) ) ;
#138362=CARTESIAN_POINT ( 'NONE',  ( 6.005480084712508493, 28.92564299267933947, 4.000000000000000000 ) ) ;
#138363=CARTESIAN_POINT ( 'NONE',  ( 4.499999999999972466, 21.43112307739196609, 4.000000000000000000 ) ) ;
#138364=VECTOR ( 'NONE', #22887, 1000.000000000000227 ) ;
#138365=ORIENTED_EDGE ( 'NONE', *, *, #76244, .T. ) ;
#138366=LINE ( 'NONE', #136214, #134606 ) ;
#138367=EDGE_LOOP ( 'NONE', ( #21630, #31012, #91097 ) ) ;
#138368=DIRECTION ( 'NONE',  ( -0.7071067811865487940, 0.7071067811865463515, 0.000000000000000000 ) ) ;
#138369=CARTESIAN_POINT ( 'NONE',  ( -27.18398860626900060, 28.73617430169806042, 5.000000000000000000 ) ) ;
#138371=VECTOR ( 'NONE', #15797, 999.9999999999998863 ) ;
#138372=CARTESIAN_POINT ( 'NONE',  ( -15.79289321881334551, -5.240707523384225297, 5.000000000000000000 ) ) ;
#138373=DIRECTION ( 'NONE',  ( -0.7071067811865487940, 0.7071067811865463515, 0.000000000000000000 ) ) ;
#138374=FACE_OUTER_BOUND ( 'NONE', #8605, .T. ) ;
#138375=DIRECTION ( 'NONE',  ( -0.7071067811865487940, 0.7071067811865463515, -0.000000000000000000 ) ) ;
#138376=CARTESIAN_POINT ( 'NONE',  ( -27.75860074219777118, 21.72500000000000142, 5.000000000000000000 ) ) ;
#138379=CARTESIAN_POINT ( 'NONE',  ( -16.80981832425541356, -18.74070752338408852, 7.910009926591547114 ) ) ;
#138380=CARTESIAN_POINT ( 'NONE',  ( 34.42499999999998295, 7.541399257801974620, 5.000000000000000000 ) ) ;
#138381=CARTESIAN_POINT ( 'NONE',  ( 34.49999999999975842, 15.05432934483078888, 4.994342998332163219 ) ) ;
#138382=ORIENTED_EDGE ( 'NONE', *, *, #111751, .F. ) ;
#138383=ORIENTED_EDGE ( 'NONE', *, *, #113442, .F. ) ;
#138387=ORIENTED_EDGE ( 'NONE', *, *, #4742, .T. ) ;
#138389=EDGE_CURVE ( 'NONE', #12163, #41563, #60782, .T. ) ;
#138390=LINE ( 'NONE', #125382, #106526 ) ;
#138391=LINE ( 'NONE', #140516, #131108 ) ;
#138393=PLANE ( 'NONE',  #101920 ) ;
#138394=CARTESIAN_POINT ( 'NONE',  ( -9.707106781186480404, 17.25929247661554911, 5.000000000000000000 ) ) ;
#138396=EDGE_CURVE ( 'NONE', #27314, #141369, #28107, .T. ) ;
#138397=CARTESIAN_POINT ( 'NONE',  ( -11.99999999999991296, 1.931123077392161935, 4.000000000000000000 ) ) ;
#138398=AXIS2_PLACEMENT_3D ( 'NONE', #121510, #9140, #130994 ) ;
#138399=DIRECTION ( 'NONE',  ( -0.000000000000000000, -0.3543493200069152693, 0.9351131265310292928 ) ) ;
#138401=EDGE_CURVE ( 'NONE', #94913, #105827, #41119, .T. ) ;
#138402=DIRECTION ( 'NONE',  ( 0.6830127018922180770, -0.6830127018922204085, -0.2588190451025213501 ) ) ;
#138403=DIRECTION ( 'NONE',  ( 1.000000000000000000, 0.000000000000000000, 0.000000000000000000 ) ) ;
#138404=CARTESIAN_POINT ( 'NONE',  ( -10.62823445044378268, -8.240707523384203981, 11.38925528200755011 ) ) ;
#138405=DIRECTION ( 'NONE',  ( 0.3543493200069163240, 0.000000000000000000, 0.9351131265310288487 ) ) ;
#138407=CARTESIAN_POINT ( 'NONE',  ( 15.48921356237309510, -27.52281430457066236, 5.000000000000000000 ) ) ;
#138410=EDGE_CURVE ( 'NONE', #131245, #89344, #6539, .T. ) ;
#138412=ORIENTED_EDGE ( 'NONE', *, *, #107449, .T. ) ;
#138413=ORIENTED_EDGE ( 'NONE', *, *, #48125, .T. ) ;
#138415=VECTOR ( 'NONE', #53224, 999.9999999999998863 ) ;
#138417=EDGE_CURVE ( 'NONE', #27246, #142384, #117926, .T. ) ;
#138418=PLANE ( 'NONE',  #131241 ) ;
#138419=ADVANCED_FACE ( 'NONE', ( #7754 ), #74490, .F. ) ;
#138420=DIRECTION ( 'NONE',  ( -0.7071067811865487940, 0.7071067811865463515, 0.000000000000000000 ) ) ;
#138422=DIRECTION ( 'NONE',  ( -0.7071067811865486830, -0.7071067811865464625, -0.000000000000000000 ) ) ;
#138424=ADVANCED_FACE ( 'NONE', ( #135908 ), #125025, .F. ) ;
#138425=VECTOR ( 'NONE', #103774, 1000.000000000000000 ) ;
#138427=ORIENTED_EDGE ( 'NONE', *, *, #126232, .T. ) ;
#138428=FACE_OUTER_BOUND ( 'NONE', #49443, .T. ) ;
#138429=ORIENTED_EDGE ( 'NONE', *, *, #62999, .F. ) ;
#138430=CARTESIAN_POINT ( 'NONE',  ( 28.17183060077627843, -17.24070752338409918, 4.000000000000000000 ) ) ;
#138431=DIRECTION ( 'NONE',  ( 0.7071067811865487940, 0.7071067811865463515, 0.000000000000000000 ) ) ;
#138432=CARTESIAN_POINT ( 'NONE',  ( 32.47599861414528277, 22.03583458319438648, 4.979811245910084061 ) ) ;
#138434=CARTESIAN_POINT ( 'NONE',  ( -15.48921356237309510, -27.52281430457066236, 5.000000000000000000 ) ) ;
#138435=ADVANCED_FACE ( 'NONE', ( #127157 ), #35915, .F. ) ;
#138436=ORIENTED_EDGE ( 'NONE', *, *, #19281, .T. ) ;
#138437=EDGE_LOOP ( 'NONE', ( #103721, #10866, #118808, #6556 ) ) ;
#138438=VECTOR ( 'NONE', #100309, 1000.000000000000000 ) ;
#138439=ORIENTED_EDGE ( 'NONE', *, *, #44796, .T. ) ;
#138440=CARTESIAN_POINT ( 'NONE',  ( -15.18398860626900237, 28.73617430169797871, 5.000000000000000000 ) ) ;
#138441=CARTESIAN_POINT ( 'NONE',  ( -57.29974487139158157, -27.71228299555246011, 4.000000000000000000 ) ) ;
#138443=ADVANCED_FACE ( 'NONE', ( #48915 ), #69241, .T. ) ;
#138445=CARTESIAN_POINT ( 'NONE',  ( -24.48921356237309510, -27.52281430457072631, 5.000000000000000000 ) ) ;
#138446=DIRECTION ( 'NONE',  ( -0.000000000000000000, -0.000000000000000000, 1.000000000000000000 ) ) ;
#138447=ORIENTED_EDGE ( 'NONE', *, *, #141757, .F. ) ;
#138448=ORIENTED_EDGE ( 'NONE', *, *, #10527, .T. ) ;
#138449=DIRECTION ( 'NONE',  ( 0.7071067811865487940, -0.7071067811865463515, 0.000000000000000000 ) ) ;
#138450=ORIENTED_EDGE ( 'NONE', *, *, #107001, .T. ) ;
#138451=ORIENTED_EDGE ( 'NONE', *, *, #97038, .T. ) ;
#138454=EDGE_CURVE ( 'NONE', #5991, #19902, #3912, .T. ) ;
#138455=PLANE ( 'NONE',  #4881 ) ;
#138457=VERTEX_POINT ( 'NONE', #24983 ) ;
#138458=CARTESIAN_POINT ( 'NONE',  ( 17.99999999999987566, -12.41253812416062985, 4.000000000000000000 ) ) ;
#138459=EDGE_CURVE ( 'NONE', #94920, #62368, #115535, .T. ) ;
#138460=LINE ( 'NONE', #72534, #140455 ) ;
#138461=LINE ( 'NONE', #53600, #76134 ) ;
#138462=DIRECTION ( 'NONE',  ( -0.000000000000000000, 0.3543493200069153248, 0.9351131265310292928 ) ) ;
#138463=ORIENTED_EDGE ( 'NONE', *, *, #134826, .F. ) ;
#138464=VECTOR ( 'NONE', #73466, 1000.000000000000000 ) ;
#138465=EDGE_CURVE ( 'NONE', #72863, #12885, #3233, .T. ) ;
#138466=LINE ( 'NONE', #105792, #104220 ) ;
#138467=FACE_BOUND ( 'NONE', #20821, .T. ) ;
#138468=VERTEX_POINT ( 'NONE', #59107 ) ;
#138469=FACE_OUTER_BOUND ( 'NONE', #137631, .T. ) ;
#138470=DIRECTION ( 'NONE',  ( 0.3543493200069162685, -0.000000000000000000, -0.9351131265310288487 ) ) ;
#138471=PLANE ( 'NONE',  #32990 ) ;
#138472=ORIENTED_EDGE ( 'NONE', *, *, #34693, .T. ) ;
#138474=ORIENTED_EDGE ( 'NONE', *, *, #11063, .T. ) ;
#138475=VECTOR ( 'NONE', #121164, 1000.000000000000000 ) ;
#138476=ORIENTED_EDGE ( 'NONE', *, *, #46836, .T. ) ;
#138477=EDGE_CURVE ( 'NONE', #102772, #82836, #103263, .T. ) ;
#138478=ORIENTED_EDGE ( 'NONE', *, *, #84442, .T. ) ;
#138480=VERTEX_POINT ( 'NONE', #135226 ) ;
#138481=CARTESIAN_POINT ( 'NONE',  ( -39.48921356237310221, -27.52281430457082934, 5.000000000000000000 ) ) ;
#138482=DIRECTION ( 'NONE',  ( 0.7071067811865487940, 0.7071067811865463515, -0.000000000000000000 ) ) ;
#138483=CARTESIAN_POINT ( 'NONE',  ( 0.7071067811865398012, -15.74070752338413115, 5.000000000000000000 ) ) ;
#138484=EDGE_CURVE ( 'NONE', #47660, #77866, #47524, .T. ) ;
#138485=CARTESIAN_POINT ( 'NONE',  ( 36.18398860626899705, 28.73617430169812437, 5.000000000000000000 ) ) ;
#138488=( BOUNDED_CURVE ( )  B_SPLINE_CURVE ( 3, ( #61969, #49675, #5393, #106125 ),
 .UNSPECIFIED., .F., .F. ) 
 B_SPLINE_CURVE_WITH_KNOTS ( ( 4, 4 ),
 ( 4.350170835173026163, 4.500739107949192075 ),
 .UNSPECIFIED. ) 
 CURVE ( )  GEOMETRIC_REPRESENTATION_ITEM ( )  RATIONAL_B_SPLINE_CURVE ( ( 1.000000000000000000, 0.9981116584018963067, 0.9981116584018963067, 1.000000000000000000 ) ) 
 REPRESENTATION_ITEM ( '' )  );
#138489=DIRECTION ( 'NONE',  ( 0.7071067811865487940, 0.7071067811865463515, 0.000000000000000000 ) ) ;
#138490=VECTOR ( 'NONE', #45326, 1000.000000000000000 ) ;
#138492=LINE ( 'NONE', #29009, #103830 ) ;
#138493=DIRECTION ( 'NONE',  ( 0.6830127018922180770, -0.6830127018922204085, -0.2588190451025213501 ) ) ;
#138494=ORIENTED_EDGE ( 'NONE', *, *, #138589, .T. ) ;
#138495=VERTEX_POINT ( 'NONE', #113423 ) ;
#138496=ORIENTED_EDGE ( 'NONE', *, *, #88595, .T. ) ;
#138497=ORIENTED_EDGE ( 'NONE', *, *, #121527, .F. ) ;
#138498=LINE ( 'NONE', #118869, #105016 ) ;
#138501=FACE_OUTER_BOUND ( 'NONE', #31912, .T. ) ;
#138502=ADVANCED_FACE ( 'NONE', ( #103959 ), #72119, .F. ) ;
#138503=LINE ( 'NONE', #93568, #85623 ) ;
#138504=ORIENTED_EDGE ( 'NONE', *, *, #18023, .T. ) ;
#138505=CARTESIAN_POINT ( 'NONE',  ( 28.17665910159955800, 5.259292476615669010, 15.86257073897091452 ) ) ;
#138506=ORIENTED_EDGE ( 'NONE', *, *, #54268, .T. ) ;
#138507=CARTESIAN_POINT ( 'NONE',  ( 34.92499999999997584, 20.71849043720405348, 4.759050581649322709 ) ) ;
#138508=ADVANCED_FACE ( 'NONE', ( #125763 ), #26436, .F. ) ;
#138509=DIRECTION ( 'NONE',  ( -0.000000000000000000, -0.3543493200069152693, 0.9351131265310292928 ) ) ;
#138511=ORIENTED_EDGE ( 'NONE', *, *, #81944, .T. ) ;
#138513=DIRECTION ( 'NONE',  ( 0.7071067811865487940, -0.7071067811865463515, 0.000000000000000000 ) ) ;
#138514=CARTESIAN_POINT ( 'NONE',  ( 15.98911971346040062, -22.02621442084248216, 4.990779571109220214 ) ) ;
#138515=CARTESIAN_POINT ( 'NONE',  ( 20.99999999999985789, -8.151047557385048492, -8.977947279169846695 ) ) ;
#138516=ORIENTED_EDGE ( 'NONE', *, *, #133030, .F. ) ;
#138517=EDGE_LOOP ( 'NONE', ( #125329, #108497, #37429, #83295 ) ) ;
#138518=LINE ( 'NONE', #39205, #14871 ) ;
#138519=ORIENTED_EDGE ( 'NONE', *, *, #42876, .T. ) ;
#138521=LINE ( 'NONE', #127647, #125041 ) ;
#138522=PLANE ( 'NONE',  #17559 ) ;
#138523=CARTESIAN_POINT ( 'NONE',  ( 3.183988606268992161, 28.73617430169789699, 5.000000000000000000 ) ) ;
#138524=CARTESIAN_POINT ( 'NONE',  ( -20.99999999999984368, 4.384688058510544550, -7.090945410444732033 ) ) ;
#138525=ORIENTED_EDGE ( 'NONE', *, *, #138147, .F. ) ;
#138526=ADVANCED_FACE ( 'NONE', ( #59791 ), #82265, .F. ) ;
#138527=CARTESIAN_POINT ( 'NONE',  ( -22.17183060077632106, 15.75929247661555443, 4.000000000000000000 ) ) ;
#138530=DIRECTION ( 'NONE',  ( -0.7071067811865486830, -0.7071067811865464625, -0.000000000000000000 ) ) ;
#138531=ORIENTED_EDGE ( 'NONE', *, *, #91600, .T. ) ;
#138532=CARTESIAN_POINT ( 'NONE',  ( -34.42500000000001137, -21.72500000000000142, 4.500000000000000888 ) ) ;
#138533=AXIS2_PLACEMENT_3D ( 'NONE', #7909, #131144, #31829 ) ;
#138535=DIRECTION ( 'NONE',  ( -0.7071067811865487940, 0.7071067811865463515, -0.000000000000000000 ) ) ;
#138536=ORIENTED_EDGE ( 'NONE', *, *, #68873, .T. ) ;
#138537=VECTOR ( 'NONE', #119008, 1000.000000000000000 ) ;
#138538=LINE ( 'NONE', #139273, #134289 ) ;
#138539=VERTEX_POINT ( 'NONE', #2502 ) ;
#138540=EDGE_CURVE ( 'NONE', #47195, #35346, #46817, .T. ) ;
#138541=ORIENTED_EDGE ( 'NONE', *, *, #88229, .T. ) ;
#138543=AXIS2_PLACEMENT_3D ( 'NONE', #21699, #110113, #86258 ) ;
#138544=ORIENTED_EDGE ( 'NONE', *, *, #47193, .F. ) ;
#138545=LINE ( 'NONE', #39235, #48920 ) ;
#138546=AXIS2_PLACEMENT_3D ( 'NONE', #45611, #142747, #12216 ) ;
#138547=CARTESIAN_POINT ( 'NONE',  ( 26.16170612452603095, -6.740707523384216415, 16.75550250614873704 ) ) ;
#138548=EDGE_LOOP ( 'NONE', ( #28669, #24117, #133183, #21967 ) ) ;
#138549=DIRECTION ( 'NONE',  ( 0.7071067811865487940, -0.7071067811865463515, 0.000000000000000000 ) ) ;
#138550=DIRECTION ( 'NONE',  ( -0.7071067811865486830, -0.7071067811865464625, -0.000000000000000000 ) ) ;
#138551=DIRECTION ( 'NONE',  ( 0.7071067811865486830, -0.7071067811865464625, -0.000000000000000000 ) ) ;
#138552=DIRECTION ( 'NONE',  ( -0.7071067811865487940, 0.7071067811865463515, -0.000000000000000000 ) ) ;
#138554=LINE ( 'NONE', #140672, #74456 ) ;
#138555=VECTOR ( 'NONE', #12631, 1000.000000000000227 ) ;
#138556=CARTESIAN_POINT ( 'NONE',  ( 29.99999999999979039, 16.55218569542899587, 5.000000000000000000 ) ) ;
#138557=DIRECTION ( 'NONE',  ( 0.7071067811865487940, 0.7071067811865463515, -0.000000000000000000 ) ) ;
#138558=FACE_OUTER_BOUND ( 'NONE', #92617, .T. ) ;
#138559=ORIENTED_EDGE ( 'NONE', *, *, #70748, .T. ) ;
#138561=ORIENTED_EDGE ( 'NONE', *, *, #16145, .F. ) ;
#138563=VECTOR ( 'NONE', #138373, 1000.000000000000000 ) ;
#138564=ORIENTED_EDGE ( 'NONE', *, *, #139650, .T. ) ;
#138565=ORIENTED_EDGE ( 'NONE', *, *, #72655, .F. ) ;
#138566=ORIENTED_EDGE ( 'NONE', *, *, #2288, .F. ) ;
#138567=DIRECTION ( 'NONE',  ( -0.6830127018922180770, -0.6830127018922204085, -0.2588190451025213501 ) ) ;
#138568=AXIS2_PLACEMENT_3D ( 'NONE', #13712, #24614, #102907 ) ;
#138569=EDGE_CURVE ( 'NONE', #1190, #47403, #58403, .T. ) ;
#138570=DIRECTION ( 'NONE',  ( -0.7071067811865486830, -0.7071067811865464625, -0.000000000000000000 ) ) ;
#138571=ORIENTED_EDGE ( 'NONE', *, *, #78606, .T. ) ;
#138572=CARTESIAN_POINT ( 'NONE',  ( -1.171830600776462061, 0.7592924766157069794, 4.000000000000000000 ) ) ;
#138573=DIRECTION ( 'NONE',  ( 0.7071067811865486830, -0.7071067811865464625, -0.000000000000000000 ) ) ;
#138574=VECTOR ( 'NONE', #118117, 1000.000000000000000 ) ;
#138575=CARTESIAN_POINT ( 'NONE',  ( 34.96659967656956525, 6.759292476615656575, 12.28218704918530157 ) ) ;
#138576=PLANE ( 'NONE',  #78916 ) ;
#138578=EDGE_LOOP ( 'NONE', ( #39194, #7364, #82008 ) ) ;
#138579=ADVANCED_FACE ( 'NONE', ( #46019 ), #101075, .F. ) ;
#138582=DIRECTION ( 'NONE',  ( -0.7071067811865487940, 0.7071067811865463515, -0.000000000000000000 ) ) ;
#138584=CARTESIAN_POINT ( 'NONE',  ( 21.48921356237309155, -27.52281430457070499, 5.000000000000000000 ) ) ;
#138585=DIRECTION ( 'NONE',  ( 0.6830127018922181881, 0.6830127018922202975, -0.2588190451025214056 ) ) ;
#138588=ADVANCED_FACE ( 'NONE', ( #12637 ), #124266, .F. ) ;
#138589=EDGE_CURVE ( 'NONE', #86852, #111653, #24248, .T. ) ;
#138590=CARTESIAN_POINT ( 'NONE',  ( -1.499999999999987566, 4.466399257802216027, 5.000000000000000000 ) ) ;
#138594=EDGE_CURVE ( 'NONE', #125403, #87604, #135863, .T. ) ;
#138595=VERTEX_POINT ( 'NONE', #35146 ) ;
#138596=CARTESIAN_POINT ( 'NONE',  ( -48.18398860626899705, 28.73617430169820608, 5.000000000000000000 ) ) ;
#138597=EDGE_CURVE ( 'NONE', #25329, #78673, #25659, .T. ) ;
#138598=CYLINDRICAL_SURFACE ( 'NONE', #64087, 0.5000000000000004441 ) ;
#138600=ADVANCED_FACE ( 'NONE', ( #34407 ), #124977, .F. ) ;
#138602=CARTESIAN_POINT ( 'NONE',  ( 34.49999999999976552, 22.01701374228158414, 2.453858888625551682 ) ) ;
#138603=VECTOR ( 'NONE', #11019, 1000.000000000000000 ) ;
#138604=LINE ( 'NONE', #66054, #92936 ) ;
#138605=CARTESIAN_POINT ( 'NONE',  ( -34.49999999999974420, -12.08601207473291161, -10.46905243149086040 ) ) ;
#138606=EDGE_CURVE ( 'NONE', #132022, #9514, #36544, .T. ) ;
#138608=ORIENTED_EDGE ( 'NONE', *, *, #75384, .T. ) ;
#138609=EDGE_CURVE ( 'NONE', #115069, #108682, #113371, .T. ) ;
#138610=DIRECTION ( 'NONE',  ( 0.7071067811865486830, -0.7071067811865464625, -0.000000000000000000 ) ) ;
#138611=ORIENTED_EDGE ( 'NONE', *, *, #90930, .T. ) ;
#138613=CARTESIAN_POINT ( 'NONE',  ( 30.48921356237309510, -27.52281430457076894, 5.000000000000000000 ) ) ;
#138615=EDGE_CURVE ( 'NONE', #56866, #102362, #114106, .T. ) ;
#138617=ORIENTED_EDGE ( 'NONE', *, *, #122596, .T. ) ;
#138619=EDGE_CURVE ( 'NONE', #12982, #59289, #4558, .T. ) ;
#138620=ORIENTED_EDGE ( 'NONE', *, *, #114383, .T. ) ;
#138622=DIRECTION ( 'NONE',  ( 0.7071067811865486830, -0.7071067811865464625, -0.000000000000000000 ) ) ;
#138623=LINE ( 'NONE', #83538, #133483 ) ;
#138624=DIRECTION ( 'NONE',  ( -0.3543493200069162685, -0.000000000000000000, -0.9351131265310288487 ) ) ;
#138625=EDGE_CURVE ( 'NONE', #47652, #46980, #3189, .T. ) ;
#138628=VERTEX_POINT ( 'NONE', #90950 ) ;
#138629=LINE ( 'NONE', #39320, #139152 ) ;
#138631=ORIENTED_EDGE ( 'NONE', *, *, #92325, .F. ) ;
#138632=ORIENTED_EDGE ( 'NONE', *, *, #43197, .T. ) ;
#138633=LINE ( 'NONE', #26999, #90993 ) ;
#138634=VERTEX_POINT ( 'NONE', #37264 ) ;
#138635=DIRECTION ( 'NONE',  ( -0.6830127018922181881, 0.6830127018922202975, -0.2588190451025214056 ) ) ;
#138636=VERTEX_POINT ( 'NONE', #57610 ) ;
#138637=DIRECTION ( 'NONE',  ( 0.7071067811865486830, -0.7071067811865464625, -0.000000000000000000 ) ) ;
#138638=ADVANCED_FACE ( 'NONE', ( #46767 ), #135178, .F. ) ;
#138639=CARTESIAN_POINT ( 'NONE',  ( 11.99999999999991296, 4.965500833774338929, -4.007596771432684335 ) ) ;
#138640=VECTOR ( 'NONE', #59164, 1000.000000000000000 ) ;
#138641=AXIS2_PLACEMENT_3D ( 'NONE', #129580, #108515, #86819 ) ;
#138642=VECTOR ( 'NONE', #118829, 1000.000000000000000 ) ;
#138643=LINE ( 'NONE', #39336, #76685 ) ;
#138644=VECTOR ( 'NONE', #5040, 1000.000000000000114 ) ;
#138645=FACE_BOUND ( 'NONE', #49426, .T. ) ;
#138647=LINE ( 'NONE', #139387, #28203 ) ;
#138648=CARTESIAN_POINT ( 'NONE',  ( 0.000000000000000000, 4.384688058510565867, -7.090945410444685848 ) ) ;
#138649=VERTEX_POINT ( 'NONE', #102539 ) ;
#138650=CARTESIAN_POINT ( 'NONE',  ( 12.18398860626900060, 28.73617430169795739, 5.000000000000000000 ) ) ;
#138651=LINE ( 'NONE', #136485, #87515 ) ;
#138652=EDGE_LOOP ( 'NONE', ( #106770, #114757, #27853, #5330 ) ) ;
#138653=ORIENTED_EDGE ( 'NONE', *, *, #95309, .T. ) ;
#138654=AXIS2_PLACEMENT_3D ( 'NONE', #94782, #37589, #40453 ) ;
#138655=AXIS2_PLACEMENT_3D ( 'NONE', #127105, #7455, #117632 ) ;
#138656=CARTESIAN_POINT ( 'NONE',  ( 26.99999999999981526, 9.631307414974347836, -9.079085613539479738 ) ) ;
#138657=EDGE_CURVE ( 'NONE', #63684, #89873, #91641, .T. ) ;
#138658=ORIENTED_EDGE ( 'NONE', *, *, #47925, .F. ) ;
#138659=ORIENTED_EDGE ( 'NONE', *, *, #95539, .T. ) ;
#138661=ORIENTED_EDGE ( 'NONE', *, *, #43953, .T. ) ;
#138663=DIRECTION ( 'NONE',  ( 0.7071067811865487940, 0.7071067811865463515, -0.000000000000000000 ) ) ;
#138664=EDGE_CURVE ( 'NONE', #13692, #105661, #59062, .T. ) ;
#138665=ORIENTED_EDGE ( 'NONE', *, *, #13916, .F. ) ;
#138666=DIRECTION ( 'NONE',  ( 0.7071067811865487940, 0.7071067811865463515, -0.000000000000000000 ) ) ;
#138667=VECTOR ( 'NONE', #115139, 1000.000000000000114 ) ;
#138670=EDGE_CURVE ( 'NONE', #99164, #36084, #103215, .T. ) ;
#138671=CARTESIAN_POINT ( 'NONE',  ( 44.99451991528749772, 28.92564299267969474, 4.000000000000000000 ) ) ;
#138672=DIRECTION ( 'NONE',  ( 0.7071067811865487940, 0.7071067811865463515, 0.000000000000000000 ) ) ;
#138673=PLANE ( 'NONE',  #135018 ) ;
#138676=AXIS2_PLACEMENT_3D ( 'NONE', #16765, #104478, #6550 ) ;
#138678=AXIS2_PLACEMENT_3D ( 'NONE', #97568, #110567, #10547 ) ;
#138679=CARTESIAN_POINT ( 'NONE',  ( -34.49999999999975131, 1.087461875839228931, 4.000000000000000000 ) ) ;
#138681=ORIENTED_EDGE ( 'NONE', *, *, #49954, .F. ) ;
#138682=AXIS2_PLACEMENT_3D ( 'NONE', #118734, #86122, #28887 ) ;
#138684=VECTOR ( 'NONE', #64356, 1000.000000000000000 ) ;
#138685=ORIENTED_EDGE ( 'NONE', *, *, #128341, .T. ) ;
#138686=DIRECTION ( 'NONE',  ( -0.7071067811865487940, 0.7071067811865463515, 0.000000000000000000 ) ) ;
#138687=CARTESIAN_POINT ( 'NONE',  ( 45.48921356237309510, -27.52281430457087197, 5.000000000000000000 ) ) ;
#138688=EDGE_CURVE ( 'NONE', #62399, #103400, #48146, .T. ) ;
#138692=CARTESIAN_POINT ( 'NONE',  ( -8.282422613574265569, -21.73023691814493219, 5.000000000000000888 ) ) ;
#138693=VECTOR ( 'NONE', #45456, 1000.000000000000000 ) ;
#138696=DIRECTION ( 'NONE',  ( 0.6830127018922180770, -0.6830127018922204085, -0.2588190451025213501 ) ) ;
#138697=VERTEX_POINT ( 'NONE', #61211 ) ;
#138698=LINE ( 'NONE', #116919, #84557 ) ;
#138700=LINE ( 'NONE', #81477, #84556 ) ;
#138702=CARTESIAN_POINT ( 'NONE',  ( -51.48921356237309510, -27.52281430457091460, 5.000000000000000000 ) ) ;
#138703=ORIENTED_EDGE ( 'NONE', *, *, #23051, .T. ) ;
#138704=DIRECTION ( 'NONE',  ( 0.6830127018922181881, 0.6830127018922202975, -0.2588190451025214056 ) ) ;
#138705=ORIENTED_EDGE ( 'NONE', *, *, #128746, .T. ) ;
#138706=DIRECTION ( 'NONE',  ( 0.6830127018922180770, -0.6830127018922204085, -0.2588190451025213501 ) ) ;
#138708=FACE_OUTER_BOUND ( 'NONE', #103594, .T. ) ;
#138709=ORIENTED_EDGE ( 'NONE', *, *, #101268, .F. ) ;
#138710=EDGE_CURVE ( 'NONE', #34731, #115267, #51721, .T. ) ;
#138711=LINE ( 'NONE', #39395, #142218 ) ;
#138713=CARTESIAN_POINT ( 'NONE',  ( -17.81601139373099940, 28.73617430169775133, 5.000000000000000000 ) ) ;
#138714=ORIENTED_EDGE ( 'NONE', *, *, #126130, .T. ) ;
#138715=DIRECTION ( 'NONE',  ( 1.000000000000000000, 0.000000000000000000, 0.000000000000000000 ) ) ;
#138716=DIRECTION ( 'NONE',  ( 0.7071067811865487940, 0.7071067811865463515, 0.000000000000000000 ) ) ;
#138718=LINE ( 'NONE', #51711, #86509 ) ;
#138719=ORIENTED_EDGE ( 'NONE', *, *, #58095, .F. ) ;
#138720=EDGE_CURVE ( 'NONE', #14551, #24719, #104646, .T. ) ;
#138721=VERTEX_POINT ( 'NONE', #138008 ) ;
#138722=CARTESIAN_POINT ( 'NONE',  ( -25.49999999999982236, 6.431123077392117082, 4.000000000000000000 ) ) ;
#138723=( BOUNDED_CURVE ( )  B_SPLINE_CURVE ( 3, ( #22748, #33693, #40461, #19392 ),
 .UNSPECIFIED., .F., .T. ) 
 B_SPLINE_CURVE_WITH_KNOTS ( ( 4, 4 ),
 ( 1.208578181583236821, 1.359146454359482892 ),
 .UNSPECIFIED. ) 
 CURVE ( )  GEOMETRIC_REPRESENTATION_ITEM ( )  RATIONAL_B_SPLINE_CURVE ( ( 1.000000000000000000, 0.9981116584018941973, 0.9981116584018941973, 1.000000000000000000 ) ) 
 REPRESENTATION_ITEM ( '' )  );
#138725=CARTESIAN_POINT ( 'NONE',  ( 0.000000000000000000, 0.000000000000000000, 5.000000000000000000 ) ) ;
#138726=CARTESIAN_POINT ( 'NONE',  ( 57.48921356237308800, -27.52281430457095368, 5.000000000000000000 ) ) ;
#138727=CARTESIAN_POINT ( 'NONE',  ( -19.49999999999985789, -17.56887692260763245, 4.000000000000000000 ) ) ;
#138728=DIRECTION ( 'NONE',  ( 0.7071067811865487940, -0.7071067811865463515, 0.000000000000000000 ) ) ;
#138729=VERTEX_POINT ( 'NONE', #50290 ) ;
#138730=DIRECTION ( 'NONE',  ( -0.7071067811865486830, -0.7071067811865464625, 0.000000000000000000 ) ) ;
#138732=DIRECTION ( 'NONE',  ( 0.6830127018922181881, 0.6830127018922202975, -0.2588190451025214056 ) ) ;
#138733=CARTESIAN_POINT ( 'NONE',  ( 0.1839886062690032631, 28.73617430169787568, 5.000000000000000000 ) ) ;
#138739=ORIENTED_EDGE ( 'NONE', *, *, #84611, .T. ) ;
#138740=CARTESIAN_POINT ( 'NONE',  ( -9.005480084712511157, 28.92564299267931816, 4.000000000000000000 ) ) ;
#138741=VECTOR ( 'NONE', #49360, 1000.000000000000000 ) ;
#138742=VECTOR ( 'NONE', #125714, 1000.000000000000000 ) ;
#138743=VECTOR ( 'NONE', #117015, 1000.000000000000000 ) ;
#138745=DIRECTION ( 'NONE',  ( 0.7071067811865486830, -0.7071067811865464625, -0.000000000000000000 ) ) ;
#138746=EDGE_CURVE ( 'NONE', #27605, #63895, #115485, .T. ) ;
#138747=AXIS2_PLACEMENT_3D ( 'NONE', #60024, #15055, #27353 ) ;
#138748=PLANE ( 'NONE',  #62536 ) ;
#138750=DIRECTION ( 'NONE',  ( -0.6830127018922181881, 0.6830127018922202975, -0.2588190451025214056 ) ) ;
#138752=CARTESIAN_POINT ( 'NONE',  ( 13.17183060077638501, 12.75929247661559351, 4.000000000000000000 ) ) ;
#138753=PLANE ( 'NONE',  #116263 ) ;
#138755=AXIS2_PLACEMENT_3D ( 'NONE', #10155, #118918, #9407 ) ;
#138756=FACE_OUTER_BOUND ( 'NONE', #87090, .T. ) ;
#138757=DIRECTION ( 'NONE',  ( -0.7071067811865486830, -0.7071067811865464625, 0.000000000000000000 ) ) ;
#138758=LINE ( 'NONE', #29258, #59685 ) ;
#138760=ADVANCED_FACE ( 'NONE', ( #62591 ), #63331, .F. ) ;
#138761=CARTESIAN_POINT ( 'NONE',  ( 19.37176554955603436, -8.240707523384200428, 11.38925528200748083 ) ) ;
#138762=ORIENTED_EDGE ( 'NONE', *, *, #13588, .T. ) ;
#138766=EDGE_CURVE ( 'NONE', #22463, #94800, #73468, .T. ) ;
#138767=PLANE ( 'NONE',  #129544 ) ;
#138770=VECTOR ( 'NONE', #85907, 1000.000000000000000 ) ;
#138771=EDGE_LOOP ( 'NONE', ( #111024, #27494, #120663, #39523 ) ) ;
#138772=ADVANCED_FACE ( 'NONE', ( #52402 ), #137299, .T. ) ;
#138773=DIRECTION ( 'NONE',  ( -0.6830127018922180770, -0.6830127018922204085, -0.2588190451025213501 ) ) ;
#138777=DIRECTION ( 'NONE',  ( -0.6830127018922180770, -0.6830127018922204085, -0.2588190451025213501 ) ) ;
#138778=ORIENTED_EDGE ( 'NONE', *, *, #104009, .T. ) ;
#138779=ORIENTED_EDGE ( 'NONE', *, *, #114842, .T. ) ;
#138781=VECTOR ( 'NONE', #118990, 1000.000000000000000 ) ;
#138783=DIRECTION ( 'NONE',  ( 0.000000000000000000, 0.3543493200069153248, 0.9351131265310291818 ) ) ;
#138784=PLANE ( 'NONE',  #53578 ) ;
#138785=VECTOR ( 'NONE', #139994, 1000.000000000000000 ) ;
#138786=EDGE_CURVE ( 'NONE', #75123, #64810, #18317, .T. ) ;
#138787=DIRECTION ( 'NONE',  ( 0.7071067811865487940, -0.7071067811865463515, 0.000000000000000000 ) ) ;
#138788=EDGE_CURVE ( 'NONE', #69645, #66281, #84365, .T. ) ;
#138789=CARTESIAN_POINT ( 'NONE',  ( 13.49999999999990763, 19.46639925780206326, 5.000000000000000000 ) ) ;
#138790=DIRECTION ( 'NONE',  ( -0.000000000000000000, 0.000000000000000000, 1.000000000000000000 ) ) ;
#138791=EDGE_LOOP ( 'NONE', ( #30100, #58947, #99065, #103488 ) ) ;
#138792=VECTOR ( 'NONE', #117529, 1000.000000000000000 ) ;
#138793=LINE ( 'NONE', #39480, #87753 ) ;
#138794=DIRECTION ( 'NONE',  ( 0.7071067811865487940, -0.7071067811865463515, 0.000000000000000000 ) ) ;
#138795=CARTESIAN_POINT ( 'NONE',  ( -5.999999999999952927, 2.587461875839218273, 4.000000000000000000 ) ) ;
#138797=DIRECTION ( 'NONE',  ( -0.3543493200069162685, -0.000000000000000000, -0.9351131265310288487 ) ) ;
#138798=VECTOR ( 'NONE', #87359, 1000.000000000000000 ) ;
#138799=EDGE_CURVE ( 'NONE', #54517, #137275, #27087, .T. ) ;
#138800=ORIENTED_EDGE ( 'NONE', *, *, #110418, .T. ) ;
#138801=ORIENTED_EDGE ( 'NONE', *, *, #81092, .F. ) ;
#138802=DIRECTION ( 'NONE',  ( -0.7071067811865487940, 0.7071067811865463515, 0.000000000000000000 ) ) ;
#138803=DIRECTION ( 'NONE',  ( -0.7071067811865486830, -0.7071067811865464625, 0.000000000000000000 ) ) ;
#138804=CARTESIAN_POINT ( 'NONE',  ( 41.99451991528749062, 28.92564299267967343, 4.000000000000000000 ) ) ;
#138806=LINE ( 'NONE', #117026, #54835 ) ;
#138807=VERTEX_POINT ( 'NONE', #106776 ) ;
#138808=ORIENTED_EDGE ( 'NONE', *, *, #55110, .F. ) ;
#138809=EDGE_CURVE ( 'NONE', #130071, #9641, #94477, .T. ) ;
#138810=DIRECTION ( 'NONE',  ( 0.7071067811865487940, 0.7071067811865463515, 0.000000000000000000 ) ) ;
#138811=LINE ( 'NONE', #27163, #139382 ) ;
#138812=ORIENTED_EDGE ( 'NONE', *, *, #108773, .F. ) ;
#138813=ORIENTED_EDGE ( 'NONE', *, *, #66637, .T. ) ;
#138814=CARTESIAN_POINT ( 'NONE',  ( -20.39513766812466855, 21.75929247661549937, 21.32995629748191035 ) ) ;
#138816=CARTESIAN_POINT ( 'NONE',  ( 31.49999999999978684, -1.912538124160739095, 4.000000000000000000 ) ) ;
#138817=EDGE_CURVE ( 'NONE', #75424, #65015, #72071, .T. ) ;
#138818=CARTESIAN_POINT ( 'NONE',  ( -29.84387692260737879, -22.22500000000000142, 4.000000000000000000 ) ) ;
#138819=FACE_BOUND ( 'NONE', #102610, .T. ) ;
#138820=DIRECTION ( 'NONE',  ( -0.6830127018922181881, 0.6830127018922202975, -0.2588190451025214056 ) ) ;
#138821=DIRECTION ( 'NONE',  ( 0.6830127018922180770, -0.6830127018922204085, -0.2588190451025214056 ) ) ;
#138822=DIRECTION ( 'NONE',  ( 0.3543493200069162685, -0.000000000000000000, -0.9351131265310288487 ) ) ;
#138823=ORIENTED_EDGE ( 'NONE', *, *, #106150, .T. ) ;
#138826=EDGE_CURVE ( 'NONE', #109128, #14910, #71328, .T. ) ;
#138827=ORIENTED_EDGE ( 'NONE', *, *, #49249, .F. ) ;
#138828=ORIENTED_EDGE ( 'NONE', *, *, #72524, .T. ) ;
#138830=VERTEX_POINT ( 'NONE', #85038 ) ;
#138831=CARTESIAN_POINT ( 'NONE',  ( 34.92499999999998295, 22.22500000000000142, 4.500000000000000888 ) ) ;
#138832=LINE ( 'NONE', #114884, #81788 ) ;
#138833=DIRECTION ( 'NONE',  ( -0.7071067811865487940, 0.7071067811865463515, 0.000000000000000000 ) ) ;
#138834=CARTESIAN_POINT ( 'NONE',  ( -29.99451991528749417, 28.92564299267958816, 4.000000000000000000 ) ) ;
#138835=VERTEX_POINT ( 'NONE', #138727 ) ;
#138836=CARTESIAN_POINT ( 'NONE',  ( 11.99999999999991296, 16.55218569542899587, 5.000000000000000000 ) ) ;
#138837=DIRECTION ( 'NONE',  ( -0.7071067811865487940, 0.7071067811865463515, -0.000000000000000000 ) ) ;
#138838=EDGE_CURVE ( 'NONE', #50212, #64365, #24580, .T. ) ;
#138839=FACE_OUTER_BOUND ( 'NONE', #75016, .T. ) ;
#138840=CARTESIAN_POINT ( 'NONE',  ( -31.49999999999977973, 10.46639925780216096, 5.000000000000000000 ) ) ;
#138841=LINE ( 'NONE', #94589, #100603 ) ;
#138842=FACE_OUTER_BOUND ( 'NONE', #68912, .T. ) ;
#138843=FACE_OUTER_BOUND ( 'NONE', #64137, .T. ) ;
#138845=VECTOR ( 'NONE', #12453, 1000.000000000000227 ) ;
#138846=CARTESIAN_POINT ( 'NONE',  ( 15.55937119539439806, -22.22500000000000142, 24.13041545083173034 ) ) ;
#138847=VECTOR ( 'NONE', #25556, 1000.000000000000000 ) ;
#138848=VERTEX_POINT ( 'NONE', #39417 ) ;
#138849=DIRECTION ( 'NONE',  ( 0.6830127018922180770, -0.6830127018922204085, -0.2588190451025213501 ) ) ;
#138850=CARTESIAN_POINT ( 'NONE',  ( -25.49999999999982236, 15.05218569542901896, 5.000000000000000000 ) ) ;
#138851=VECTOR ( 'NONE', #116899, 1000.000000000000000 ) ;
#138852=VERTEX_POINT ( 'NONE', #28540 ) ;
#138853=VERTEX_POINT ( 'NONE', #72798 ) ;
#138854=EDGE_CURVE ( 'NONE', #48007, #64418, #116952, .T. ) ;
#138855=VERTEX_POINT ( 'NONE', #106048 ) ;
#138857=ORIENTED_EDGE ( 'NONE', *, *, #48087, .F. ) ;
#138862=EDGE_LOOP ( 'NONE', ( #87743, #60487, #99979, #7231 ) ) ;
#138863=PLANE ( 'NONE',  #112906 ) ;
#138864=ORIENTED_EDGE ( 'NONE', *, *, #80488, .T. ) ;
#138865=CARTESIAN_POINT ( 'NONE',  ( -12.18398860626900060, 28.73617430169795739, 5.000000000000000000 ) ) ;
#138867=CARTESIAN_POINT ( 'NONE',  ( 9.328169399223460445, 17.25929247661554911, 4.000000000000000000 ) ) ;
#138868=PLANE ( 'NONE',  #47117 ) ;
#138870=EDGE_LOOP ( 'NONE', ( #84367, #7620, #10937, #81634 ) ) ;
#138874=VECTOR ( 'NONE', #6233, 1000.000000000000114 ) ;
#138875=CARTESIAN_POINT ( 'NONE',  ( 21.18398860626899349, 28.73617430169802134, 5.000000000000000000 ) ) ;
#138876=VERTEX_POINT ( 'NONE', #6715 ) ;
#138877=EDGE_CURVE ( 'NONE', #66944, #116320, #95193, .T. ) ;
#138878=VERTEX_POINT ( 'NONE', #32091 ) ;
#138880=ORIENTED_EDGE ( 'NONE', *, *, #25789, .T. ) ;
#138881=DIRECTION ( 'NONE',  ( -0.000000000000000000, 0.3543493200069153248, 0.9351131265310292928 ) ) ;
#138882=VECTOR ( 'NONE', #58410, 999.9999999999998863 ) ;
#138883=VECTOR ( 'NONE', #38543, 1000.000000000000000 ) ;
#138884=DIRECTION ( 'NONE',  ( -0.000000000000000000, 0.000000000000000000, 1.000000000000000000 ) ) ;
#138885=VECTOR ( 'NONE', #131066, 1000.000000000000227 ) ;
#138886=DIRECTION ( 'NONE',  ( 0.7071067811865486830, -0.7071067811865464625, -0.000000000000000000 ) ) ;
#138887=EDGE_CURVE ( 'NONE', #15770, #59525, #76319, .T. ) ;
#138888=DIRECTION ( 'NONE',  ( -0.000000000000000000, 0.3543493200069153248, 0.9351131265310292928 ) ) ;
#138889=ORIENTED_EDGE ( 'NONE', *, *, #24165, .F. ) ;
#138892=DIRECTION ( 'NONE',  ( -0.6830127018922180770, -0.6830127018922204085, -0.2588190451025213501 ) ) ;
#138894=AXIS2_PLACEMENT_3D ( 'NONE', #104689, #48179, #15503 ) ;
#138895=CARTESIAN_POINT ( 'NONE',  ( 15.79289321881335084, -17.24070752338411339, 5.000000000000000000 ) ) ;
#138897=CARTESIAN_POINT ( 'NONE',  ( -19.05000000000000071, 3.174999999999997158, 4.000000000000000000 ) ) ;
#138899=DIRECTION ( 'NONE',  ( 0.7071067811865487940, -0.7071067811865463515, 0.000000000000000000 ) ) ;
#138900=VERTEX_POINT ( 'NONE', #33550 ) ;
#138901=ORIENTED_EDGE ( 'NONE', *, *, #119882, .F. ) ;
#138902=ORIENTED_EDGE ( 'NONE', *, *, #2345, .F. ) ;
#138903=LINE ( 'NONE', #29398, #83413 ) ;
#138904=LINE ( 'NONE', #51897, #104345 ) ;
#138909=EDGE_CURVE ( 'NONE', #32788, #68309, #55283, .T. ) ;
#138910=DIRECTION ( 'NONE',  ( -0.3543493200069162685, -0.000000000000000000, -0.9351131265310288487 ) ) ;
#138911=DIRECTION ( 'NONE',  ( -0.000000000000000000, 0.3543493200069153248, 0.9351131265310292928 ) ) ;
#138913=CARTESIAN_POINT ( 'NONE',  ( 8.999999999999932498, -16.02097659208071079, -11.96015758381210858 ) ) ;
#138914=CARTESIAN_POINT ( 'NONE',  ( 20.67183060077632817, 11.25929247661560950, 4.000000000000000000 ) ) ;
#138915=ORIENTED_EDGE ( 'NONE', *, *, #3760, .T. ) ;
#138916=AXIS2_PLACEMENT_3D ( 'NONE', #72757, #116911, #94437 ) ;
#138917=LINE ( 'NONE', #39615, #142514 ) ;
#138918=ORIENTED_EDGE ( 'NONE', *, *, #7640, .T. ) ;
#138919=DIRECTION ( 'NONE',  ( -0.7071067811865486830, -0.7071067811865464625, 0.000000000000000000 ) ) ;
#138920=CARTESIAN_POINT ( 'NONE',  ( 34.49999999999975842, -16.53574439159934073, 4.994342998332164107 ) ) ;
#138921=ORIENTED_EDGE ( 'NONE', *, *, #64017, .F. ) ;
#138922=LINE ( 'NONE', #51198, #127410 ) ;
#138923=CARTESIAN_POINT ( 'NONE',  ( -18.41161490594819128, 22.22500000000000497, 4.777194822843813249 ) ) ;
#138924=ORIENTED_EDGE ( 'NONE', *, *, #83151, .T. ) ;
#138925=EDGE_LOOP ( 'NONE', ( #16410, #74724, #127372, #35370 ) ) ;
#138926=LINE ( 'NONE', #39627, #67500 ) ;
#138927=CARTESIAN_POINT ( 'NONE',  ( 6.792893218813413014, -11.24070752338416668, 5.000000000000000000 ) ) ;
#138929=LINE ( 'NONE', #119285, #19511 ) ;
#138931=DIRECTION ( 'NONE',  ( 0.7071067811865487940, 0.7071067811865463515, 0.000000000000000000 ) ) ;
#138932=EDGE_CURVE ( 'NONE', #12211, #126178, #97306, .T. ) ;
#138934=ORIENTED_EDGE ( 'NONE', *, *, #29931, .F. ) ;
#138936=ADVANCED_FACE ( 'NONE', ( #98067 ), #86487, .F. ) ;
#138937=DIRECTION ( 'NONE',  ( 0.6830127018922181881, 0.6830127018922202975, -0.2588190451025214056 ) ) ;
#138939=DIRECTION ( 'NONE',  ( 0.7071067811865487940, 0.7071067811865463515, 0.000000000000000000 ) ) ;
#138940=EDGE_LOOP ( 'NONE', ( #123772, #121918, #33148 ) ) ;
#138941=EDGE_CURVE ( 'NONE', #69925, #15594, #109645, .T. ) ;
#138942=EDGE_CURVE ( 'NONE', #23069, #58856, #8843, .T. ) ;
#138943=DIRECTION ( 'NONE',  ( -0.6830127018922180770, -0.6830127018922204085, -0.2588190451025213501 ) ) ;
#138944=ORIENTED_EDGE ( 'NONE', *, *, #140564, .F. ) ;
#138945=VECTOR ( 'NONE', #109257, 999.9999999999998863 ) ;
#138948=LINE ( 'NONE', #138222, #88648 ) ;
#138949=CARTESIAN_POINT ( 'NONE',  ( -7.499999999999951150, 0.4311230773921780335, 4.000000000000000000 ) ) ;
#138950=VERTEX_POINT ( 'NONE', #88629 ) ;
#138951=VECTOR ( 'NONE', #99415, 1000.000000000000000 ) ;
#138952=VECTOR ( 'NONE', #61023, 1000.000000000000000 ) ;
#138953=VECTOR ( 'NONE', #87700, 1000.000000000000000 ) ;
#138954=DIRECTION ( 'NONE',  ( -0.000000000000000000, -0.3543493200069152693, 0.9351131265310292928 ) ) ;
#138955=( BOUNDED_CURVE ( )  B_SPLINE_CURVE ( 3, ( #67820, #92354, #137326, #59083 ),
 .UNSPECIFIED., .F., .T. ) 
 B_SPLINE_CURVE_WITH_KNOTS ( ( 4, 4 ),
 ( 5.005968288816728951, 5.074607125596323876 ),
 .UNSPECIFIED. ) 
 CURVE ( )  GEOMETRIC_REPRESENTATION_ITEM ( )  RATIONAL_B_SPLINE_CURVE ( ( 1.000000000000000000, 0.9996074310407766506, 0.9996074310407766506, 1.000000000000000000 ) ) 
 REPRESENTATION_ITEM ( '' )  );
#138956=DIRECTION ( 'NONE',  ( -0.000000000000000000, -0.3543493200069152693, 0.9351131265310292928 ) ) ;
#138958=CARTESIAN_POINT ( 'NONE',  ( 33.70710678118631165, 8.259292476615639700, 5.000000000000000000 ) ) ;
#138959=ADVANCED_FACE ( 'NONE', ( #44428 ), #75606, .F. ) ;
#138961=VERTEX_POINT ( 'NONE', #108902 ) ;
#138962=LINE ( 'NONE', #104138, #76171 ) ;
#138963=CARTESIAN_POINT ( 'NONE',  ( 2.999999999999985345, 5.587461875839184522, 4.000000000000000000 ) ) ;
#138964=AXIS2_PLACEMENT_3D ( 'NONE', #29427, #117842, #119981 ) ;
#138969=ORIENTED_EDGE ( 'NONE', *, *, #73675, .F. ) ;
#138970=ADVANCED_FACE ( 'NONE', ( #77751 ), #42275, .T. ) ;
#138971=VECTOR ( 'NONE', #108565, 1000.000000000000000 ) ;
#138972=CARTESIAN_POINT ( 'NONE',  ( -2.149948714589740462, -8.240707523384200428, 17.25253755692238400 ) ) ;
#138973=CARTESIAN_POINT ( 'NONE',  ( -35.75830541574791255, 0.7592924766157104211, 14.37146558664990970 ) ) ;
#138974=ORIENTED_EDGE ( 'NONE', *, *, #5213, .T. ) ;
#138975=ADVANCED_FACE ( 'NONE', ( #85743 ), #30682, .F. ) ;
#138976=DIRECTION ( 'NONE',  ( 0.7071067811865486830, -0.7071067811865464625, -0.000000000000000000 ) ) ;
#138977=PLANE ( 'NONE',  #132346 ) ;
#138978=AXIS2_PLACEMENT_3D ( 'NONE', #85804, #131470, #31442 ) ;
#138979=ORIENTED_EDGE ( 'NONE', *, *, #113439, .T. ) ;
#138980=CARTESIAN_POINT ( 'NONE',  ( 21.48921356237309155, -27.52281430457070499, 5.000000000000000000 ) ) ;
#138982=DIRECTION ( 'NONE',  ( -0.000000000000000000, 0.000000000000000000, 1.000000000000000000 ) ) ;
#138983=EDGE_CURVE ( 'NONE', #106767, #129767, #53868, .T. ) ;
#138984=DIRECTION ( 'NONE',  ( -0.7071067811865486830, -0.7071067811865464625, 0.000000000000000000 ) ) ;
#138985=VECTOR ( 'NONE', #114280, 1000.000000000000000 ) ;
#138986=VERTEX_POINT ( 'NONE', #140828 ) ;
#138988=AXIS2_PLACEMENT_3D ( 'NONE', #116422, #62064, #95371 ) ;
#138989=DIRECTION ( 'NONE',  ( -0.7071067811865486830, -0.7071067811865464625, -0.000000000000000000 ) ) ;
#138990=PLANE ( 'NONE',  #131901 ) ;
#138991=EDGE_CURVE ( 'NONE', #60821, #128385, #98754, .T. ) ;
#138992=CARTESIAN_POINT ( 'NONE',  ( 0.2997448713915885632, -27.71228299555206220, 4.000000000000000000 ) ) ;
#138993=DIRECTION ( 'NONE',  ( -0.000000000000000000, 0.3543493200069153248, 0.9351131265310292928 ) ) ;
#138995=DIRECTION ( 'NONE',  ( 0.000000000000000000, 0.000000000000000000, 1.000000000000000000 ) ) ;
#138996=DIRECTION ( 'NONE',  ( -0.3543493200069162685, -0.000000000000000000, -0.9351131265310288487 ) ) ;
#138997=EDGE_CURVE ( 'NONE', #131795, #96830, #132138, .T. ) ;
#138998=ORIENTED_EDGE ( 'NONE', *, *, #92720, .T. ) ;
#138999=EDGE_LOOP ( 'NONE', ( #93852, #124737, #2561, #25187 ) ) ;
#139000=VERTEX_POINT ( 'NONE', #11013 ) ;
#139001=ORIENTED_EDGE ( 'NONE', *, *, #7950, .F. ) ;
#139002=VECTOR ( 'NONE', #80803, 1000.000000000000000 ) ;
#139003=CARTESIAN_POINT ( 'NONE',  ( 56.99451991528749062, 28.92564299267978001, 4.000000000000000000 ) ) ;
#139004=VERTEX_POINT ( 'NONE', #21920 ) ;
#139006=CARTESIAN_POINT ( 'NONE',  ( 2.999999999999978240, -16.60178936734448385, 0.8616154019347568305 ) ) ;
#139007=PLANE ( 'NONE',  #31810 ) ;
#139009=AXIS2_PLACEMENT_3D ( 'NONE', #55073, #10115, #89816 ) ;
#139011=VERTEX_POINT ( 'NONE', #66165 ) ;
#139012=DIRECTION ( 'NONE',  ( -0.7071067811865486830, 0.7071067811865464625, 0.000000000000000000 ) ) ;
#139013=LINE ( 'NONE', #118673, #16465 ) ;
#139014=ORIENTED_EDGE ( 'NONE', *, *, #18591, .T. ) ;
#139015=CARTESIAN_POINT ( 'NONE',  ( 20.30673006690388505, -3.740707523384244837, 12.88036043432862954 ) ) ;
#139016=ORIENTED_EDGE ( 'NONE', *, *, #121183, .F. ) ;
#139018=ORIENTED_EDGE ( 'NONE', *, *, #98340, .F. ) ;
#139021=AXIS2_PLACEMENT_3D ( 'NONE', #8353, #30882, #9813 ) ;
#139022=ORIENTED_EDGE ( 'NONE', *, *, #71021, .F. ) ;
#139023=FACE_OUTER_BOUND ( 'NONE', #12257, .T. ) ;
#139024=PLANE ( 'NONE',  #65851 ) ;
#139026=LINE ( 'NONE', #39730, #28612 ) ;
#139028=FACE_OUTER_BOUND ( 'NONE', #88823, .T. ) ;
#139029=PLANE ( 'NONE',  #61498 ) ;
#139030=VECTOR ( 'NONE', #100402, 1000.000000000000000 ) ;
#139031=PLANE ( 'NONE',  #33129 ) ;
#139033=VECTOR ( 'NONE', #131150, 1000.000000000000000 ) ;
#139035=VECTOR ( 'NONE', #59812, 1000.000000000000227 ) ;
#139036=ORIENTED_EDGE ( 'NONE', *, *, #92771, .T. ) ;
#139037=DIRECTION ( 'NONE',  ( 1.000000000000000000, 0.000000000000000000, 0.000000000000000000 ) ) ;
#139039=ORIENTED_EDGE ( 'NONE', *, *, #112198, .F. ) ;
#139040=DIRECTION ( 'NONE',  ( 0.7071067811865487940, 0.7071067811865463515, 0.000000000000000000 ) ) ;
#139041=VECTOR ( 'NONE', #25269, 1000.000000000000000 ) ;
#139042=ORIENTED_EDGE ( 'NONE', *, *, #24859, .T. ) ;
#139043=VECTOR ( 'NONE', #25283, 1000.000000000000227 ) ;
#139044=AXIS2_PLACEMENT_3D ( 'NONE', #91766, #135991, #134593 ) ;
#139045=LINE ( 'NONE', #28854, #580 ) ;
#139046=PLANE ( 'NONE',  #6176 ) ;
#139047=ADVANCED_FACE ( 'NONE', ( #68332 ), #112503, .F. ) ;
#139049=LINE ( 'NONE', #121382, #83481 ) ;
#139050=ORIENTED_EDGE ( 'NONE', *, *, #455, .F. ) ;
#139051=ADVANCED_FACE ( 'NONE', ( #134267 ), #125538, .F. ) ;
#139053=AXIS2_PLACEMENT_3D ( 'NONE', #101477, #81180, #12324 ) ;
#139054=ORIENTED_EDGE ( 'NONE', *, *, #125969, .F. ) ;
#139056=DIRECTION ( 'NONE',  ( 0.3543493200069162685, -0.000000000000000000, -0.9351131265310288487 ) ) ;
#139057=FACE_OUTER_BOUND ( 'NONE', #55783, .T. ) ;
#139058=EDGE_CURVE ( 'NONE', #1414, #68140, #14619, .T. ) ;
#139059=DIRECTION ( 'NONE',  ( -0.7071067811865486830, -0.7071067811865464625, 0.000000000000000000 ) ) ;
#139060=ORIENTED_EDGE ( 'NONE', *, *, #131282, .T. ) ;
#139062=ORIENTED_EDGE ( 'NONE', *, *, #99933, .T. ) ;
#139063=DIRECTION ( 'NONE',  ( 0.3543493200069163795, -9.265275131829747941E-33, -0.9351131265310288487 ) ) ;
#139064=AXIS2_PLACEMENT_3D ( 'NONE', #106971, #75101, #51907 ) ;
#139065=DIRECTION ( 'NONE',  ( -0.000000000000000000, 0.3543493200069153248, 0.9351131265310292928 ) ) ;
#139066=FACE_OUTER_BOUND ( 'NONE', #121214, .T. ) ;
#139067=LINE ( 'NONE', #130337, #35810 ) ;
#139068=CARTESIAN_POINT ( 'NONE',  ( -14.29289321881335795, -18.74070752338409562, 5.000000000000000000 ) ) ;
#139069=DIRECTION ( 'NONE',  ( -0.7071067811865486830, 0.7071067811865464625, 0.000000000000000000 ) ) ;
#139072=VECTOR ( 'NONE', #1663, 999.9999999999998863 ) ;
#139073=CARTESIAN_POINT ( 'NONE',  ( -39.29974487139159578, -27.71228299555233576, 4.000000000000000000 ) ) ;
#139076=AXIS2_PLACEMENT_3D ( 'NONE', #70513, #24106, #125569 ) ;
#139077=VERTEX_POINT ( 'NONE', #46591 ) ;
#139078=DIRECTION ( 'NONE',  ( -0.7071067811865487940, 0.7071067811865463515, -0.000000000000000000 ) ) ;
#139079=EDGE_CURVE ( 'NONE', #83776, #119750, #90776, .T. ) ;
#139080=LINE ( 'NONE', #27426, #137376 ) ;
#139081=VECTOR ( 'NONE', #35879, 999.9999999999998863 ) ;
#139083=CARTESIAN_POINT ( 'NONE',  ( -5.671830600776429421, 17.25929247661554911, 4.000000000000000000 ) ) ;
#139084=DIRECTION ( 'NONE',  ( 1.000000000000000000, 0.000000000000000000, 0.000000000000000000 ) ) ;
#139085=ORIENTED_EDGE ( 'NONE', *, *, #31327, .F. ) ;
#139086=VECTOR ( 'NONE', #20656, 1000.000000000000227 ) ;
#139087=FACE_OUTER_BOUND ( 'NONE', #90478, .T. ) ;
#139088=LINE ( 'NONE', #120137, #131828 ) ;
#139089=EDGE_CURVE ( 'NONE', #95876, #54517, #135692, .T. ) ;
#139090=ORIENTED_EDGE ( 'NONE', *, *, #44607, .F. ) ;
#139091=PLANE ( 'NONE',  #51292 ) ;
#139092=ADVANCED_FACE ( 'NONE', ( #114628 ), #36379, .F. ) ;
#139095=DIRECTION ( 'NONE',  ( 0.7071067811865486830, -0.7071067811865464625, -0.000000000000000000 ) ) ;
#139097=CARTESIAN_POINT ( 'NONE',  ( 54.48921356237310221, -27.52281430457093236, 5.000000000000000000 ) ) ;
#139099=LINE ( 'NONE', #118001, #62196 ) ;
#139100=CARTESIAN_POINT ( 'NONE',  ( -45.48921356237309510, -27.52281430457087197, 5.000000000000000000 ) ) ;
#139101=DIRECTION ( 'NONE',  ( -0.3543493200069162685, -0.000000000000000000, -0.9351131265310288487 ) ) ;
#139102=EDGE_CURVE ( 'NONE', #12275, #83894, #133555, .T. ) ;
#139103=LINE ( 'NONE', #41191, #55276 ) ;
#139107=CARTESIAN_POINT ( 'NONE',  ( 29.99999999999979750, -10.44781430457071814, 5.000000000000000000 ) ) ;
#139108=CARTESIAN_POINT ( 'NONE',  ( 6.489213562373093325, -27.52281430457059841, 5.000000000000000000 ) ) ;
#139110=EDGE_LOOP ( 'NONE', ( #35280, #130840, #26165, #50867 ) ) ;
#139111=EDGE_CURVE ( 'NONE', #94938, #48357, #58900, .T. ) ;
#139112=EDGE_LOOP ( 'NONE', ( #6511, #71427, #65584, #16148 ) ) ;
#139113=ADVANCED_FACE ( 'NONE', ( #103060 ), #3696, .F. ) ;
#139115=ORIENTED_EDGE ( 'NONE', *, *, #47240, .F. ) ;
#139120=ORIENTED_EDGE ( 'NONE', *, *, #9603, .T. ) ;
#139121=FACE_OUTER_BOUND ( 'NONE', #62823, .T. ) ;
#139122=EDGE_CURVE ( 'NONE', #85885, #14857, #122653, .T. ) ;
#139123=DIRECTION ( 'NONE',  ( 0.7071067811865487940, 0.7071067811865463515, 0.000000000000000000 ) ) ;
#139124=PLANE ( 'NONE',  #14011 ) ;
#139125=CARTESIAN_POINT ( 'NONE',  ( -32.67183060077625356, -21.74070752338406010, 4.000000000000000000 ) ) ;
#139126=EDGE_CURVE ( 'NONE', #126258, #81493, #5128, .T. ) ;
#139127=EDGE_CURVE ( 'NONE', #96060, #15871, #71885, .T. ) ;
#139129=CARTESIAN_POINT ( 'NONE',  ( 0.000000000000000000, 0.000000000000000000, 5.000000000000000000 ) ) ;
#139130=PLANE ( 'NONE',  #45729 ) ;
#139131=CARTESIAN_POINT ( 'NONE',  ( 30.79289321881324781, -5.240707523384230626, 5.000000000000000000 ) ) ;
#139132=AXIS2_PLACEMENT_3D ( 'NONE', #70662, #48885, #15488 ) ;
#139133=PLANE ( 'NONE',  #28498 ) ;
#139134=CARTESIAN_POINT ( 'NONE',  ( 13.49999999999991473, 3.073033219394640803, -6.593910359670939414 ) ) ;
#139135=LINE ( 'NONE', #105741, #56847 ) ;
#139136=( BOUNDED_CURVE ( )  B_SPLINE_CURVE ( 3, ( #24467, #55156, #143555, #21803 ),
 .UNSPECIFIED., .F., .T. ) 
 B_SPLINE_CURVE_WITH_KNOTS ( ( 4, 4 ),
 ( 2.779374508378132713, 4.199602562396797190 ),
 .UNSPECIFIED. ) 
 CURVE ( )  GEOMETRIC_REPRESENTATION_ITEM ( )  RATIONAL_B_SPLINE_CURVE ( ( 1.000000000000000000, 0.8388583629366712646, 0.8388583629366712646, 1.000000000000000000 ) ) 
 REPRESENTATION_ITEM ( '' )  );
#139138=VERTEX_POINT ( 'NONE', #61719 ) ;
#139139=ORIENTED_EDGE ( 'NONE', *, *, #19927, .T. ) ;
#139141=ORIENTED_EDGE ( 'NONE', *, *, #72908, .F. ) ;
#139142=EDGE_CURVE ( 'NONE', #91989, #115804, #95742, .T. ) ;
#139144=DIRECTION ( 'NONE',  ( -0.7071067811865486830, -0.7071067811865464625, 0.000000000000000000 ) ) ;
#139145=CARTESIAN_POINT ( 'NONE',  ( 25.49999999999982236, 18.05218569542898521, 5.000000000000000000 ) ) ;
#139146=VERTEX_POINT ( 'NONE', #126926 ) ;
#139147=VECTOR ( 'NONE', #80413, 1000.000000000000000 ) ;
#139148=EDGE_CURVE ( 'NONE', #67859, #123554, #7280, .T. ) ;
#139149=FACE_OUTER_BOUND ( 'NONE', #74620, .T. ) ;
#139150=DIRECTION ( 'NONE',  ( 0.7071067811865486830, -0.7071067811865464625, -0.000000000000000000 ) ) ;
#139152=VECTOR ( 'NONE', #84271, 1000.000000000000000 ) ;
#139154=ORIENTED_EDGE ( 'NONE', *, *, #32906, .F. ) ;
#139155=LINE ( 'NONE', #129672, #92903 ) ;
#139156=ORIENTED_EDGE ( 'NONE', *, *, #73334, .F. ) ;
#139157=LINE ( 'NONE', #73884, #24473 ) ;
#139158=AXIS2_PLACEMENT_3D ( 'NONE', #55261, #56730, #134987 ) ;
#139159=VECTOR ( 'NONE', #41543, 1000.000000000000227 ) ;
#139160=FACE_OUTER_BOUND ( 'NONE', #26554, .T. ) ;
#139161=VECTOR ( 'NONE', #56210, 1000.000000000000000 ) ;
#139162=VECTOR ( 'NONE', #88077, 1000.000000000000227 ) ;
#139163=PLANE ( 'NONE',  #1397 ) ;
#139164=DIRECTION ( 'NONE',  ( -0.000000000000000000, 0.000000000000000000, 1.000000000000000000 ) ) ;
#139166=ORIENTED_EDGE ( 'NONE', *, *, #107461, .T. ) ;
#139167=ORIENTED_EDGE ( 'NONE', *, *, #14043, .F. ) ;
#139168=ORIENTED_EDGE ( 'NONE', *, *, #52803, .T. ) ;
#139169=CARTESIAN_POINT ( 'NONE',  ( 9.758600742197899081, 21.72500000000000853, 5.000000000000000000 ) ) ;
#139170=CARTESIAN_POINT ( 'NONE',  ( 11.99451991528749417, 28.92564299267946382, 4.000000000000000000 ) ) ;
#139172=VECTOR ( 'NONE', #44847, 1000.000000000000000 ) ;
#139173=CARTESIAN_POINT ( 'NONE',  ( 25.17183060077628909, -11.24070752338417556, 4.000000000000000000 ) ) ;
#139174=ADVANCED_FACE ( 'NONE', ( #17462 ), #39240, .F. ) ;
#139175=FILL_AREA_STYLE ('',( #17363 ) ) ;
#139176=EDGE_CURVE ( 'NONE', #54517, #124390, #10587, .T. ) ;
#139178=EDGE_LOOP ( 'NONE', ( #16283, #120411, #114386, #85354 ) ) ;
#139179=VECTOR ( 'NONE', #59159, 1000.000000000000000 ) ;
#139181=CARTESIAN_POINT ( 'NONE',  ( -3.284736659904287315, 22.22500000000000142, 16.98967855471618904 ) ) ;
#139182=ORIENTED_EDGE ( 'NONE', *, *, #75340, .F. ) ;
#139183=ORIENTED_EDGE ( 'NONE', *, *, #117666, .F. ) ;
#139184=AXIS2_PLACEMENT_3D ( 'NONE', #81525, #26408, #73306 ) ;
#139186=VECTOR ( 'NONE', #28458, 1000.000000000000000 ) ;
#139187=VECTOR ( 'NONE', #128610, 1000.000000000000000 ) ;
#139188=CARTESIAN_POINT ( 'NONE',  ( -66.18398860626901126, 28.73617430169833753, 5.000000000000000000 ) ) ;
#139189=CARTESIAN_POINT ( 'NONE',  ( 21.96495920677946856, -2.033836129387410985, 4.000000000000000000 ) ) ;
#139190=EDGE_LOOP ( 'NONE', ( #58689, #40551, #118974, #29324 ) ) ;
#139191=DIRECTION ( 'NONE',  ( 0.3543493200069162685, -0.000000000000000000, -0.9351131265310288487 ) ) ;
#139193=DIRECTION ( 'NONE',  ( -0.3543493200069162685, -0.000000000000000000, -0.9351131265310288487 ) ) ;
#139194=CARTESIAN_POINT ( 'NONE',  ( 20.99999999999985789, 19.55218569542897100, 5.000000000000000000 ) ) ;
#139196=LINE ( 'NONE', #128994, #83734 ) ;
#139197=ORIENTED_EDGE ( 'NONE', *, *, #136476, .F. ) ;
#139198=LINE ( 'NONE', #28986, #116160 ) ;
#139199=CARTESIAN_POINT ( 'NONE',  ( -8.229957205422008926, 21.73644205237997795, 5.000000000000000000 ) ) ;
#139200=ORIENTED_EDGE ( 'NONE', *, *, #72946, .T. ) ;
#139202=DIRECTION ( 'NONE',  ( 0.7071067811865486830, -0.7071067811865464625, -0.000000000000000000 ) ) ;
#139204=VERTEX_POINT ( 'NONE', #105188 ) ;
#139205=LINE ( 'NONE', #72548, #89894 ) ;
#139206=ORIENTED_EDGE ( 'NONE', *, *, #17918, .T. ) ;
#139207=ORIENTED_EDGE ( 'NONE', *, *, #7118, .T. ) ;
#139208=VERTEX_POINT ( 'NONE', #50115 ) ;
#139210=VECTOR ( 'NONE', #73719, 1000.000000000000114 ) ;
#139211=DIRECTION ( 'NONE',  ( 0.6830127018922181881, 0.6830127018922202975, -0.2588190451025214056 ) ) ;
#139212=DIRECTION ( 'NONE',  ( 0.6830127018922180770, -0.6830127018922204085, -0.2588190451025213501 ) ) ;
#139215=DIRECTION ( 'NONE',  ( 0.7071067811865487940, 0.7071067811865463515, 0.000000000000000000 ) ) ;
#139216=VECTOR ( 'NONE', #139688, 1000.000000000000000 ) ;
#139217=FACE_OUTER_BOUND ( 'NONE', #86683, .T. ) ;
#139218=AXIS2_PLACEMENT_3D ( 'NONE', #101263, #67975, #120862 ) ;
#139219=CARTESIAN_POINT ( 'NONE',  ( -5.671830600776438303, 14.25929247661558286, 4.000000000000000000 ) ) ;
#139220=CARTESIAN_POINT ( 'NONE',  ( -24.18398860626899705, 28.73617430169804265, 5.000000000000000000 ) ) ;
#139221=DIRECTION ( 'NONE',  ( 0.6830127018922180770, -0.6830127018922204085, -0.2588190451025213501 ) ) ;
#139222=LINE ( 'NONE', #59522, #123526 ) ;
#139223=ORIENTED_EDGE ( 'NONE', *, *, #40854, .F. ) ;
#139225=VERTEX_POINT ( 'NONE', #6542 ) ;
#139226=VECTOR ( 'NONE', #71149, 999.9999999999998863 ) ;
#139227=EDGE_LOOP ( 'NONE', ( #34546, #48335, #94691, #20884 ) ) ;
#139228=FACE_OUTER_BOUND ( 'NONE', #141919, .T. ) ;
#139229=VERTEX_POINT ( 'NONE', #139284 ) ;
#139230=EDGE_CURVE ( 'NONE', #113151, #17161, #39976, .T. ) ;
#139231=ORIENTED_EDGE ( 'NONE', *, *, #111962, .F. ) ;
#139232=DIRECTION ( 'NONE',  ( 0.6830127018922180770, -0.6830127018922204085, -0.2588190451025213501 ) ) ;
#139233=LINE ( 'NONE', #39931, #50315 ) ;
#139234=ADVANCED_FACE ( 'NONE', ( #4382 ), #84870, .F. ) ;
#139235=EDGE_CURVE ( 'NONE', #142570, #48699, #29066, .T. ) ;
#139236=FACE_OUTER_BOUND ( 'NONE', #120525, .T. ) ;
#139238=CARTESIAN_POINT ( 'NONE',  ( 24.14562793195489121, 0.06350461447051275465, 4.871950940718897449 ) ) ;
#139239=VECTOR ( 'NONE', #91352, 1000.000000000000000 ) ;
#139240=ORIENTED_EDGE ( 'NONE', *, *, #34882, .F. ) ;
#139241=CARTESIAN_POINT ( 'NONE',  ( 34.92499999999998295, 20.81665438641024224, 4.500000000000000888 ) ) ;
#139242=EDGE_CURVE ( 'NONE', #109272, #63778, #126241, .T. ) ;
#139243=EDGE_CURVE ( 'NONE', #28105, #35225, #52240, .T. ) ;
#139244=DIRECTION ( 'NONE',  ( 1.000000000000000000, 0.000000000000000000, 0.000000000000000000 ) ) ;
#139246=ORIENTED_EDGE ( 'NONE', *, *, #101732, .T. ) ;
#139248=ADVANCED_FACE ( 'NONE', ( #121058 ), #131965, .F. ) ;
#139249=CARTESIAN_POINT ( 'NONE',  ( -59.99451991528749772, 28.92564299267980132, 4.000000000000000000 ) ) ;
#139250=DIRECTION ( 'NONE',  ( -0.7071067811865487940, 0.7071067811865463515, 0.000000000000000000 ) ) ;
#139251=VERTEX_POINT ( 'NONE', #96421 ) ;
#139254=ORIENTED_EDGE ( 'NONE', *, *, #140645, .T. ) ;
#139255=DIRECTION ( 'NONE',  ( 0.7071067811865486830, -0.7071067811865464625, -0.000000000000000000 ) ) ;
#139256=VECTOR ( 'NONE', #127277, 1000.000000000000000 ) ;
#139257=CARTESIAN_POINT ( 'NONE',  ( -34.49999999999975842, -13.53574439159936915, 4.994342998332166772 ) ) ;
#139258=CARTESIAN_POINT ( 'NONE',  ( 15.18398860626900237, 28.73617430169797871, 5.000000000000000000 ) ) ;
#139259=EDGE_LOOP ( 'NONE', ( #75938, #36024, #97208, #132149 ) ) ;
#139260=VECTOR ( 'NONE', #101025, 1000.000000000000227 ) ;
#139261=DIRECTION ( 'NONE',  ( 0.7071067811865486830, -0.7071067811865464625, -0.000000000000000000 ) ) ;
#139263=AXIS2_PLACEMENT_3D ( 'NONE', #95998, #109007, #41624 ) ;
#139264=DIRECTION ( 'NONE',  ( 0.7071067811865487940, 0.7071067811865463515, 0.000000000000000000 ) ) ;
#139265=CARTESIAN_POINT ( 'NONE',  ( -20.31999820585105709, -22.22500000000000142, 10.53438114343992105 ) ) ;
#139266=ORIENTED_EDGE ( 'NONE', *, *, #54043, .F. ) ;
#139267=CARTESIAN_POINT ( 'NONE',  ( -20.99451991528748707, 28.92564299267952777, 4.000000000000000000 ) ) ;
#139268=VECTOR ( 'NONE', #73983, 999.9999999999998863 ) ;
#139269=VECTOR ( 'NONE', #35369, 1000.000000000000000 ) ;
#139270=VECTOR ( 'NONE', #49302, 1000.000000000000227 ) ;
#139271=PLANE ( 'NONE',  #123525 ) ;
#139272=ORIENTED_EDGE ( 'NONE', *, *, #106045, .T. ) ;
#139273=CARTESIAN_POINT ( 'NONE',  ( 33.48921356237309510, -27.52281430457078670, 5.000000000000000000 ) ) ;
#139274=ORIENTED_EDGE ( 'NONE', *, *, #109865, .T. ) ;
#139275=ORIENTED_EDGE ( 'NONE', *, *, #137161, .F. ) ;
#139276=CARTESIAN_POINT ( 'NONE',  ( -14.81601139373099585, 28.73617430169776910, 5.000000000000000000 ) ) ;
#139277=AXIS2_PLACEMENT_3D ( 'NONE', #17674, #3237, #103268 ) ;
#139279=EDGE_CURVE ( 'NONE', #110441, #74437, #10846, .T. ) ;
#139280=ORIENTED_EDGE ( 'NONE', *, *, #37611, .F. ) ;
#139281=LINE ( 'NONE', #127675, #90506 ) ;
#139283=DIRECTION ( 'NONE',  ( 0.7071067811865486830, -0.7071067811865464625, -0.000000000000000000 ) ) ;
#139284=CARTESIAN_POINT ( 'NONE',  ( -32.99999999999977263, -7.068876922607736368, 4.000000000000000000 ) ) ;
#139285=VECTOR ( 'NONE', #32946, 1000.000000000000000 ) ;
#139286=CARTESIAN_POINT ( 'NONE',  ( -57.18398860626899705, 28.73617430169827358, 5.000000000000000000 ) ) ;
#139287=DIRECTION ( 'NONE',  ( 0.7071067811865487940, -0.7071067811865463515, 0.000000000000000000 ) ) ;
#139288=FACE_OUTER_BOUND ( 'NONE', #131037, .T. ) ;
#139290=EDGE_CURVE ( 'NONE', #109637, #97476, #7998, .T. ) ;
#139291=PLANE ( 'NONE',  #139184 ) ;
#139292=DIRECTION ( 'NONE',  ( 1.000000000000000000, 0.000000000000000000, 0.000000000000000000 ) ) ;
#139293=PLANE ( 'NONE',  #34454 ) ;
#139295=CARTESIAN_POINT ( 'NONE',  ( -2.671830600776452957, -6.740707523384211086, 4.000000000000000000 ) ) ;
#139296=VERTEX_POINT ( 'NONE', #64546 ) ;
#139298=ORIENTED_EDGE ( 'NONE', *, *, #10873, .F. ) ;
#139299=ORIENTED_EDGE ( 'NONE', *, *, #80030, .F. ) ;
#139300=EDGE_CURVE ( 'NONE', #13156, #58219, #42107, .T. ) ;
#139302=VECTOR ( 'NONE', #91216, 1000.000000000000000 ) ;
#139303=ORIENTED_EDGE ( 'NONE', *, *, #86194, .T. ) ;
#139305=EDGE_CURVE ( 'NONE', #126557, #41413, #30505, .T. ) ;
#139307=ORIENTED_EDGE ( 'NONE', *, *, #133494, .T. ) ;
#139308=DIRECTION ( 'NONE',  ( -0.3543493200069162685, -0.000000000000000000, -0.9351131265310288487 ) ) ;
#139310=AXIS2_PLACEMENT_3D ( 'NONE', #71714, #101459, #90605 ) ;
#139311=ORIENTED_EDGE ( 'NONE', *, *, #104208, .F. ) ;
#139312=DIRECTION ( 'NONE',  ( 0.3543493200069162685, -0.000000000000000000, -0.9351131265310288487 ) ) ;
#139313=EDGE_CURVE ( 'NONE', #54270, #131755, #86317, .T. ) ;
#139315=DIRECTION ( 'NONE',  ( 0.000000000000000000, -1.000000000000000000, 0.000000000000000000 ) ) ;
#139316=PLANE ( 'NONE',  #67425 ) ;
#139318=VERTEX_POINT ( 'NONE', #31220 ) ;
#139321=FACE_OUTER_BOUND ( 'NONE', #85877, .T. ) ;
#139323=DIRECTION ( 'NONE',  ( -0.7071067811865486830, -0.7071067811865464625, -0.000000000000000000 ) ) ;
#139324=CARTESIAN_POINT ( 'NONE',  ( 42.18398860626899705, 28.73617430169816700, 5.000000000000000000 ) ) ;
#139325=DIRECTION ( 'NONE',  ( -0.7071067811865486830, -0.7071067811865464625, 0.000000000000000000 ) ) ;
#139329=ORIENTED_EDGE ( 'NONE', *, *, #137365, .F. ) ;
#139330=EDGE_LOOP ( 'NONE', ( #140822, #38410, #120851, #6798 ) ) ;
#139332=EDGE_LOOP ( 'NONE', ( #93230, #73907, #63241, #9220 ) ) ;
#139333=EDGE_CURVE ( 'NONE', #83478, #16704, #74737, .T. ) ;
#139334=DIRECTION ( 'NONE',  ( -0.7071067811865486830, -0.7071067811865464625, 0.000000000000000000 ) ) ;
#139335=VECTOR ( 'NONE', #103791, 1000.000000000000000 ) ;
#139336=DIRECTION ( 'NONE',  ( -0.7071067811865487940, 0.7071067811865463515, -0.000000000000000000 ) ) ;
#139337=VECTOR ( 'NONE', #124100, 1000.000000000000000 ) ;
#139338=LINE ( 'NONE', #50872, #140595 ) ;
#139339=CARTESIAN_POINT ( 'NONE',  ( 31.49999999999977973, -7.533600742197658739, 5.000000000000000000 ) ) ;
#139340=CARTESIAN_POINT ( 'NONE',  ( -66.18398860626901126, 28.73617430169833753, 5.000000000000000000 ) ) ;
#139341=DIRECTION ( 'NONE',  ( -8.817971600062198362E-18, -0.3543493200069152693, 0.9351131265310292928 ) ) ;
#139344=ORIENTED_EDGE ( 'NONE', *, *, #128128, .F. ) ;
#139345=VECTOR ( 'NONE', #135476, 1000.000000000000227 ) ;
#139347=VERTEX_POINT ( 'NONE', #42819 ) ;
#139349=LINE ( 'NONE', #51609, #57771 ) ;
#139350=LINE ( 'NONE', #40725, #137942 ) ;
#139351=CARTESIAN_POINT ( 'NONE',  ( -33.79333936457824450, 21.75929247661549581, 4.998822639870701856 ) ) ;
#139353=EDGE_LOOP ( 'NONE', ( #86409, #7945, #87082, #73319 ) ) ;
#139354=EDGE_CURVE ( 'NONE', #128836, #110463, #87015, .T. ) ;
#139356=ORIENTED_EDGE ( 'NONE', *, *, #40914, .T. ) ;
#139357=PLANE ( 'NONE',  #123535 ) ;
#139359=CARTESIAN_POINT ( 'NONE',  ( -33.48921356237309510, -27.52281430457078670, 5.000000000000000000 ) ) ;
#139360=CARTESIAN_POINT ( 'NONE',  ( 32.20666063542130075, 21.75929247661549937, 4.998822639870702744 ) ) ;
#139361=VECTOR ( 'NONE', #35913, 999.9999999999998863 ) ;
#139362=EDGE_CURVE ( 'NONE', #117708, #47726, #31921, .T. ) ;
#139364=ADVANCED_FACE ( 'NONE', ( #24605 ), #55837, .F. ) ;
#139365=VERTEX_POINT ( 'NONE', #134101 ) ;
#139366=DIRECTION ( 'NONE',  ( -0.7071067811865486830, -0.7071067811865464625, -0.000000000000000000 ) ) ;
#139367=LINE ( 'NONE', #129158, #45642 ) ;
#139368=EDGE_LOOP ( 'NONE', ( #139584, #25584, #2534, #132589 ) ) ;
#139369=ORIENTED_EDGE ( 'NONE', *, *, #92487, .F. ) ;
#139370=LINE ( 'NONE', #136466, #114141 ) ;
#139371=VECTOR ( 'NONE', #67796, 1000.000000000000227 ) ;
#139373=ORIENTED_EDGE ( 'NONE', *, *, #46707, .F. ) ;
#139374=( BOUNDED_CURVE ( )  B_SPLINE_CURVE ( 3, ( #106214, #73626, #105511, #48295 ),
 .UNSPECIFIED., .F., .F. ) 
 B_SPLINE_CURVE_WITH_KNOTS ( ( 4, 4 ),
 ( 5.143245962375956992, 6.645403452391244414 ),
 .UNSPECIFIED. ) 
 CURVE ( )  GEOMETRIC_REPRESENTATION_ITEM ( )  RATIONAL_B_SPLINE_CURVE ( ( 1.000000000000000000, 0.8206354192515227242, 0.8206354192515227242, 1.000000000000000000 ) ) 
 REPRESENTATION_ITEM ( '' )  );
#139375=AXIS2_PLACEMENT_3D ( 'NONE', #133476, #34163, #2190 ) ;
#139376=ADVANCED_FACE ( 'NONE', ( #46411 ), #136219, .F. ) ;
#139378=ORIENTED_EDGE ( 'NONE', *, *, #101954, .F. ) ;
#139379=CARTESIAN_POINT ( 'NONE',  ( -34.92500000000001137, -14.24070752338414003, 4.255531930566244903 ) ) ;
#139380=VECTOR ( 'NONE', #73515, 1000.000000000000000 ) ;
#139381=AXIS2_PLACEMENT_3D ( 'NONE', #83108, #69388, #50484 ) ;
#139382=VECTOR ( 'NONE', #40226, 1000.000000000000227 ) ;
#139384=FACE_BOUND ( 'NONE', #131059, .T. ) ;
#139385=EDGE_CURVE ( 'NONE', #28277, #68408, #35531, .T. ) ;
#139386=DIRECTION ( 'NONE',  ( -0.6830127018922180770, -0.6830127018922204085, -0.2588190451025213501 ) ) ;
#139387=CARTESIAN_POINT ( 'NONE',  ( 47.99451991528749062, 28.92564299267971251, 4.000000000000000000 ) ) ;
#139388=LINE ( 'NONE', #5936, #96526 ) ;
#139389=ORIENTED_EDGE ( 'NONE', *, *, #132424, .F. ) ;
#139391=ORIENTED_EDGE ( 'NONE', *, *, #46362, .F. ) ;
#139392=ORIENTED_EDGE ( 'NONE', *, *, #72710, .T. ) ;
#139393=CARTESIAN_POINT ( 'NONE',  ( -20.81601139373100295, 28.73617430169773002, 5.000000000000000000 ) ) ;
#139394=EDGE_LOOP ( 'NONE', ( #90544, #28974, #117834, #15414 ) ) ;
#139396=ORIENTED_EDGE ( 'NONE', *, *, #92445, .T. ) ;
#139397=DIRECTION ( 'NONE',  ( 0.7071067811865487940, -0.7071067811865463515, 0.000000000000000000 ) ) ;
#139399=ORIENTED_EDGE ( 'NONE', *, *, #1632, .T. ) ;
#139401=VECTOR ( 'NONE', #102652, 1000.000000000000227 ) ;
#139402=VECTOR ( 'NONE', #95283, 1000.000000000000000 ) ;
#139403=FACE_OUTER_BOUND ( 'NONE', #113264, .T. ) ;
#139404=LINE ( 'NONE', #5258, #129178 ) ;
#139405=CARTESIAN_POINT ( 'NONE',  ( -31.49999999999977973, 7.087461875839173864, 4.000000000000000000 ) ) ;
#139407=LINE ( 'NONE', #50945, #107132 ) ;
#139409=ORIENTED_EDGE ( 'NONE', *, *, #127110, .T. ) ;
#139410=EDGE_LOOP ( 'NONE', ( #61665, #135605, #44376, #4693 ) ) ;
#139413=DIRECTION ( 'NONE',  ( -0.6830127018922180770, -0.6830127018922204085, -0.2588190451025213501 ) ) ;
#139414=VERTEX_POINT ( 'NONE', #113760 ) ;
#139415=ORIENTED_EDGE ( 'NONE', *, *, #87944, .F. ) ;
#139416=ORIENTED_EDGE ( 'NONE', *, *, #134408, .F. ) ;
#139417=DIRECTION ( 'NONE',  ( -0.7071067811865487940, 0.7071067811865463515, -0.000000000000000000 ) ) ;
#139418=ADVANCED_FACE ( 'NONE', ( #89165 ), #58731, .T. ) ;
#139419=CARTESIAN_POINT ( 'NONE',  ( 32.20710678118632586, 3.759292476615680112, 5.000000000000000000 ) ) ;
#139420=VERTEX_POINT ( 'NONE', #34080 ) ;
#139421=FACE_OUTER_BOUND ( 'NONE', #76661, .T. ) ;
#139422=EDGE_CURVE ( 'NONE', #128690, #125706, #122477, .T. ) ;
#139423=EDGE_CURVE ( 'NONE', #131140, #40695, #113029, .T. ) ;
#139424=EDGE_CURVE ( 'NONE', #133750, #40271, #77592, .T. ) ;
#139426=DIRECTION ( 'NONE',  ( 0.3543493200069163240, -0.000000000000000000, 0.9351131265310288487 ) ) ;
#139427=EDGE_CURVE ( 'NONE', #113106, #80820, #66697, .T. ) ;
#139428=ORIENTED_EDGE ( 'NONE', *, *, #12349, .T. ) ;
#139429=CARTESIAN_POINT ( 'NONE',  ( 2.999999999999975131, -22.22500000000000853, 4.412002311790043763 ) ) ;
#139430=ADVANCED_FACE ( 'NONE', ( #79032 ), #102189, .F. ) ;
#139431=CARTESIAN_POINT ( 'NONE',  ( -15.18398860626900237, 28.73617430169797871, 5.000000000000000000 ) ) ;
#139432=AXIS2_PLACEMENT_3D ( 'NONE', #62129, #61447, #117181 ) ;
#139434=CARTESIAN_POINT ( 'NONE',  ( 19.82816939922339117, -5.240707523384228850, 4.000000000000000000 ) ) ;
#139435=CARTESIAN_POINT ( 'NONE',  ( -13.49999999999990230, -4.912538124160707120, 4.000000000000000000 ) ) ;
#139439=ORIENTED_EDGE ( 'NONE', *, *, #47557, .F. ) ;
#139440=ADVANCED_FACE ( 'NONE', ( #92002 ), #2846, .F. ) ;
#139441=LINE ( 'NONE', #119753, #40383 ) ;
#139442=FACE_OUTER_BOUND ( 'NONE', #97775, .T. ) ;
#139444=VERTEX_POINT ( 'NONE', #56582 ) ;
#139445=EDGE_CURVE ( 'NONE', #17061, #68847, #100748, .T. ) ;
#139447=FACE_OUTER_BOUND ( 'NONE', #28988, .T. ) ;
#139448=DIRECTION ( 'NONE',  ( -0.7071067811865486830, -0.7071067811865464625, -0.000000000000000000 ) ) ;
#139449=VECTOR ( 'NONE', #68841, 1000.000000000000000 ) ;
#139450=ORIENTED_EDGE ( 'NONE', *, *, #112816, .T. ) ;
#139451=CARTESIAN_POINT ( 'NONE',  ( 23.99999999999983658, -10.06887692260771239, 4.000000000000000000 ) ) ;
#139452=DIRECTION ( 'NONE',  ( -0.000000000000000000, -0.3543493200069152693, 0.9351131265310292928 ) ) ;
#139453=LINE ( 'NONE', #84352, #127964 ) ;
#139454=EDGE_CURVE ( 'NONE', #125425, #86499, #47144, .T. ) ;
#139455=DIRECTION ( 'NONE',  ( 1.000000000000000000, 0.000000000000000000, 0.000000000000000000 ) ) ;
#139456=LINE ( 'NONE', #115476, #27521 ) ;
#139457=ORIENTED_EDGE ( 'NONE', *, *, #54339, .F. ) ;
#139458=ORIENTED_EDGE ( 'NONE', *, *, #137002, .T. ) ;
#139459=VECTOR ( 'NONE', #92536, 1000.000000000000000 ) ;
#139460=CARTESIAN_POINT ( 'NONE',  ( -13.82816939922343380, 15.75929247661555443, 4.000000000000000000 ) ) ;
#139462=EDGE_CURVE ( 'NONE', #49148, #104848, #14452, .T. ) ;
#139464=CARTESIAN_POINT ( 'NONE',  ( 0.1839886062690032631, 28.73617430169787568, 5.000000000000000000 ) ) ;
#139465=DIRECTION ( 'NONE',  ( 0.000000000000000000, -1.000000000000000000, 0.000000000000000000 ) ) ;
#139466=CARTESIAN_POINT ( 'NONE',  ( 17.99451991528748351, 28.92564299267950645, 4.000000000000000000 ) ) ;
#139467=VERTEX_POINT ( 'NONE', #25309 ) ;
#139468=CARTESIAN_POINT ( 'NONE',  ( -41.99451991528749062, 28.92564299267967343, 4.000000000000000000 ) ) ;
#139469=LINE ( 'NONE', #116249, #44328 ) ;
#139471=AXIS2_PLACEMENT_3D ( 'NONE', #88276, #42647, #96245 ) ;
#139472=VECTOR ( 'NONE', #91964, 999.9999999999998863 ) ;
#139474=DIRECTION ( 'NONE',  ( -0.7071067811865487940, 0.7071067811865463515, 0.000000000000000000 ) ) ;
#139476=CARTESIAN_POINT ( 'NONE',  ( 69.18398860626899705, 28.73617430169835529, 5.000000000000000000 ) ) ;
#139478=VECTOR ( 'NONE', #25396, 1000.000000000000000 ) ;
#139479=VERTEX_POINT ( 'NONE', #13000 ) ;
#139480=CARTESIAN_POINT ( 'NONE',  ( 24.29974487139158867, -27.71228299555223273, 4.000000000000000000 ) ) ;
#139482=EDGE_CURVE ( 'NONE', #74762, #64647, #101449, .T. ) ;
#139483=ORIENTED_EDGE ( 'NONE', *, *, #26518, .T. ) ;
#139484=VECTOR ( 'NONE', #91529, 1000.000000000000000 ) ;
#139485=VECTOR ( 'NONE', #73495, 1000.000000000000227 ) ;
#139486=PLANE ( 'NONE',  #121814 ) ;
#139487=EDGE_CURVE ( 'NONE', #70593, #119701, #135532, .T. ) ;
#139489=DIRECTION ( 'NONE',  ( -0.7071067811865486830, -0.7071067811865464625, 0.000000000000000000 ) ) ;
#139490=DIRECTION ( 'NONE',  ( -0.7071067811865486830, -0.7071067811865464625, 0.000000000000000000 ) ) ;
#139491=CARTESIAN_POINT ( 'NONE',  ( -32.99999999999976552, -22.22500000000000142, 4.412002311790046427 ) ) ;
#139493=ORIENTED_EDGE ( 'NONE', *, *, #127569, .T. ) ;
#139496=DIRECTION ( 'NONE',  ( 0.7071067811865486830, -0.7071067811865464625, -0.000000000000000000 ) ) ;
#139497=LINE ( 'NONE', #126422, #11449 ) ;
#139499=ADVANCED_FACE ( 'NONE', ( #26749 ), #70999, .T. ) ;
#139500=LINE ( 'NONE', #29965, #124442 ) ;
#139502=DIRECTION ( 'NONE',  ( 0.3543493200069162685, -0.000000000000000000, -0.9351131265310288487 ) ) ;
#139504=ORIENTED_EDGE ( 'NONE', *, *, #79802, .F. ) ;
#139506=DIRECTION ( 'NONE',  ( -0.000000000000000000, 0.000000000000000000, 1.000000000000000000 ) ) ;
#139507=ADVANCED_FACE ( 'NONE', ( #26049 ), #28900, .F. ) ;
#139508=CARTESIAN_POINT ( 'NONE',  ( -34.92500000000001137, -22.22500000000000142, 4.000000000000000000 ) ) ;
#139510=ORIENTED_EDGE ( 'NONE', *, *, #33742, .T. ) ;
#139511=PLANE ( 'NONE',  #69952 ) ;
#139513=AXIS2_PLACEMENT_3D ( 'NONE', #6166, #138884, #96056 ) ;
#139514=ORIENTED_EDGE ( 'NONE', *, *, #122719, .F. ) ;
#139515=LINE ( 'NONE', #94520, #24825 ) ;
#139516=ORIENTED_EDGE ( 'NONE', *, *, #20646, .T. ) ;
#139518=VECTOR ( 'NONE', #28931, 1000.000000000000000 ) ;
#139520=CARTESIAN_POINT ( 'NONE',  ( -12.32816939922344979, -0.7407075233842701500, 4.000000000000000000 ) ) ;
#139521=LINE ( 'NONE', #130040, #62904 ) ;
#139523=ADVANCED_FACE ( 'NONE', ( #127490 ), #62252, .F. ) ;
#139524=LINE ( 'NONE', #6068, #95172 ) ;
#139526=ORIENTED_EDGE ( 'NONE', *, *, #107764, .T. ) ;
#139527=ADVANCED_FACE ( 'NONE', ( #72446 ), #117304, .F. ) ;
#139528=LINE ( 'NONE', #16238, #64570 ) ;
#139529=EDGE_CURVE ( 'NONE', #13042, #70498, #103578, .T. ) ;
#139530=CARTESIAN_POINT ( 'NONE',  ( -29.58838509405148187, 22.22499999999999787, 4.777194822843818578 ) ) ;
#139531=PLANE ( 'NONE',  #56363 ) ;
#139532=CARTESIAN_POINT ( 'NONE',  ( 62.99451991528749772, 28.92564299267982264, 4.000000000000000000 ) ) ;
#139533=VERTEX_POINT ( 'NONE', #60118 ) ;
#139534=VERTEX_POINT ( 'NONE', #38351 ) ;
#139535=( BOUNDED_CURVE ( )  B_SPLINE_CURVE ( 3, ( #95501, #73763, #38994, #115795 ),
 .UNSPECIFIED., .F., .T. ) 
 B_SPLINE_CURVE_WITH_KNOTS ( ( 4, 4 ),
 ( 5.005968288816727174, 5.074607125596344304 ),
 .UNSPECIFIED. ) 
 CURVE ( )  GEOMETRIC_REPRESENTATION_ITEM ( )  RATIONAL_B_SPLINE_CURVE ( ( 1.000000000000000000, 0.9996074310407763175, 0.9996074310407763175, 1.000000000000000000 ) ) 
 REPRESENTATION_ITEM ( '' )  );
#139538=DIRECTION ( 'NONE',  ( -0.000000000000000000, 0.3543493200069153248, 0.9351131265310292928 ) ) ;
#139540=CARTESIAN_POINT ( 'NONE',  ( -51.29974487139158867, -27.71228299555242103, 4.000000000000000000 ) ) ;
#139541=CARTESIAN_POINT ( 'NONE',  ( -36.18398860626899705, 28.73617430169812437, 5.000000000000000000 ) ) ;
#139542=ORIENTED_EDGE ( 'NONE', *, *, #48825, .T. ) ;
#139543=ORIENTED_EDGE ( 'NONE', *, *, #41636, .T. ) ;
#139544=VECTOR ( 'NONE', #95408, 999.9999999999998863 ) ;
#139546=ORIENTED_EDGE ( 'NONE', *, *, #39360, .T. ) ;
#139547=ORIENTED_EDGE ( 'NONE', *, *, #49458, .F. ) ;
#139548=ADVANCED_FACE ( 'NONE', ( #104284 ), #4949, .F. ) ;
#139549=ORIENTED_EDGE ( 'NONE', *, *, #81693, .T. ) ;
#139550=DIRECTION ( 'NONE',  ( 0.000000000000000000, -0.3543493200069153248, 0.9351131265310292928 ) ) ;
#139551=VECTOR ( 'NONE', #1122, 999.9999999999998863 ) ;
#139552=FACE_BOUND ( 'NONE', #121875, .T. ) ;
#139553=ADVANCED_FACE ( 'NONE', ( #93442 ), #81891, .F. ) ;
#139555=DIRECTION ( 'NONE',  ( -1.000000000000000000, 0.000000000000000000, -0.000000000000000000 ) ) ;
#139556=AXIS2_PLACEMENT_3D ( 'NONE', #138584, #84904, #74037 ) ;
#139558=CARTESIAN_POINT ( 'NONE',  ( 21.29974487139158512, -27.71228299555221142, 4.000000000000000000 ) ) ;
#139559=VERTEX_POINT ( 'NONE', #51373 ) ;
#139561=ORIENTED_EDGE ( 'NONE', *, *, #117751, .T. ) ;
#139562=VERTEX_POINT ( 'NONE', #138372 ) ;
#139564=ORIENTED_EDGE ( 'NONE', *, *, #102443, .F. ) ;
#139565=DIRECTION ( 'NONE',  ( -0.7071067811865487940, 0.7071067811865463515, 0.000000000000000000 ) ) ;
#139566=DIRECTION ( 'NONE',  ( -0.7071067811865487940, 0.7071067811865463515, 0.000000000000000000 ) ) ;
#139567=DIRECTION ( 'NONE',  ( 0.7071067811865487940, 0.7071067811865463515, 0.000000000000000000 ) ) ;
#139568=AXIS2_PLACEMENT_3D ( 'NONE', #72785, #63319, #116938 ) ;
#139569=VECTOR ( 'NONE', #122016, 1000.000000000000227 ) ;
#139570=AXIS2_PLACEMENT_3D ( 'NONE', #20283, #117448, #107994 ) ;
#139571=AXIS2_PLACEMENT_3D ( 'NONE', #43102, #140952, #30801 ) ;
#139572=LINE ( 'NONE', #95306, #142094 ) ;
#139573=ORIENTED_EDGE ( 'NONE', *, *, #134041, .T. ) ;
#139576=DIRECTION ( 'NONE',  ( -0.7071067811865486830, -0.7071067811865464625, -0.000000000000000000 ) ) ;
#139577=DIRECTION ( 'NONE',  ( -0.6830127018922181881, 0.6830127018922202975, -0.2588190451025214056 ) ) ;
#139578=CARTESIAN_POINT ( 'NONE',  ( -0.005480084712502889671, 28.92564299267938210, 4.000000000000000000 ) ) ;
#139579=CARTESIAN_POINT ( 'NONE',  ( -29.99999999999979394, -4.068876922607771895, 4.000000000000000000 ) ) ;
#139580=VECTOR ( 'NONE', #139056, 1000.000000000000227 ) ;
#139581=AXIS2_PLACEMENT_3D ( 'NONE', #99133, #143377, #50853 ) ;
#139583=CARTESIAN_POINT ( 'NONE',  ( 42.29974487139158157, -27.71228299555235708, 4.000000000000000000 ) ) ;
#139584=ORIENTED_EDGE ( 'NONE', *, *, #18728, .F. ) ;
#139585=FACE_OUTER_BOUND ( 'NONE', #90612, .T. ) ;
#139586=LINE ( 'NONE', #51840, #9528 ) ;
#139588=ORIENTED_EDGE ( 'NONE', *, *, #48026, .T. ) ;
#139589=VERTEX_POINT ( 'NONE', #5686 ) ;
#139591=ORIENTED_EDGE ( 'NONE', *, *, #23737, .F. ) ;
#139592=EDGE_CURVE ( 'NONE', #11459, #11206, #125361, .T. ) ;
#139595=EDGE_CURVE ( 'NONE', #141889, #47375, #7096, .T. ) ;
#139596=VERTEX_POINT ( 'NONE', #17295 ) ;
#139597=ADVANCED_FACE ( 'NONE', ( #27441 ), #6369, .F. ) ;
#139598=LINE ( 'NONE', #18456, #20263 ) ;
#139599=EDGE_CURVE ( 'NONE', #28845, #5408, #48505, .T. ) ;
#139600=ORIENTED_EDGE ( 'NONE', *, *, #106262, .T. ) ;
#139601=LINE ( 'NONE', #84491, #25607 ) ;
#139603=CARTESIAN_POINT ( 'NONE',  ( 11.81601139373100651, 28.73617430169779041, 5.000000000000000000 ) ) ;
#139606=EDGE_CURVE ( 'NONE', #22337, #21537, #70311, .T. ) ;
#139608=VERTEX_POINT ( 'NONE', #39057 ) ;
#139609=CARTESIAN_POINT ( 'NONE',  ( 33.18398860626899705, 28.73617430169810305, 5.000000000000000000 ) ) ;
#139610=VERTEX_POINT ( 'NONE', #81152 ) ;
#139612=VECTOR ( 'NONE', #46754, 1000.000000000000000 ) ;
#139613=VERTEX_POINT ( 'NONE', #61559 ) ;
#139615=ORIENTED_EDGE ( 'NONE', *, *, #132469, .T. ) ;
#139616=CARTESIAN_POINT ( 'NONE',  ( -25.49999999999982236, -10.53360074219763298, 5.000000000000000000 ) ) ;
#139617=AXIS2_PLACEMENT_3D ( 'NONE', #117864, #141073, #52638 ) ;
#139618=CARTESIAN_POINT ( 'NONE',  ( 27.32816939922334143, 5.259292476615661904, 4.000000000000000000 ) ) ;
#139619=EDGE_CURVE ( 'NONE', #967, #105072, #128222, .T. ) ;
#139620=DIRECTION ( 'NONE',  ( 1.000000000000000000, 0.000000000000000000, 0.000000000000000000 ) ) ;
#139621=CARTESIAN_POINT ( 'NONE',  ( 23.99999999999982592, 8.587461875839158765, 4.000000000000000000 ) ) ;
#139623=ORIENTED_EDGE ( 'NONE', *, *, #17777, .F. ) ;
#139624=CARTESIAN_POINT ( 'NONE',  ( -21.29974487139158512, -27.71228299555221142, 4.000000000000000000 ) ) ;
#139625=ORIENTED_EDGE ( 'NONE', *, *, #66331, .T. ) ;
#139626=CARTESIAN_POINT ( 'NONE',  ( -15.18398860626900237, 28.73617430169797871, 5.000000000000000000 ) ) ;
#139627=EDGE_CURVE ( 'NONE', #132130, #130144, #84704, .T. ) ;
#139628=VECTOR ( 'NONE', #21020, 999.9999999999998863 ) ;
#139630=DIRECTION ( 'NONE',  ( 0.7071067811865486830, -0.7071067811865464625, -0.000000000000000000 ) ) ;
#139631=ORIENTED_EDGE ( 'NONE', *, *, #111734, .F. ) ;
#139633=DIRECTION ( 'NONE',  ( -0.000000000000000000, 0.000000000000000000, 1.000000000000000000 ) ) ;
#139634=ORIENTED_EDGE ( 'NONE', *, *, #89533, .F. ) ;
#139635=ORIENTED_EDGE ( 'NONE', *, *, #117727, .T. ) ;
#139636=VECTOR ( 'NONE', #79295, 1000.000000000000227 ) ;
#139637=ORIENTED_EDGE ( 'NONE', *, *, #22162, .T. ) ;
#139638=PLANE ( 'NONE',  #46402 ) ;
#139639=PLANE ( 'NONE',  #4754 ) ;
#139640=CARTESIAN_POINT ( 'NONE',  ( 0.000000000000000000, 0.000000000000000000, 5.000000000000000000 ) ) ;
#139641=VECTOR ( 'NONE', #79791, 1000.000000000000000 ) ;
#139642=CARTESIAN_POINT ( 'NONE',  ( 12.72281430457050710, -21.72500000000000142, 5.000000000000000000 ) ) ;
#139643=CARTESIAN_POINT ( 'NONE',  ( 45.18398860626900415, 28.73617430169818832, 5.000000000000000000 ) ) ;
#139645=LINE ( 'NONE', #85207, #76599 ) ;
#139646=CARTESIAN_POINT ( 'NONE',  ( 4.362461875838996583, 22.22500000000000142, 4.000000000000000000 ) ) ;
#139648=CARTESIAN_POINT ( 'NONE',  ( 63.48921356237309510, -27.52281430457099631, 5.000000000000000000 ) ) ;
#139649=LINE ( 'NONE', #137482, #78963 ) ;
#139650=EDGE_CURVE ( 'NONE', #106359, #61904, #109306, .T. ) ;
#139651=ORIENTED_EDGE ( 'NONE', *, *, #33706, .T. ) ;
#139652=AXIS2_PLACEMENT_3D ( 'NONE', #46106, #69277, #13417 ) ;
#139654=VERTEX_POINT ( 'NONE', #85395 ) ;
#139655=LINE ( 'NONE', #28733, #11331 ) ;
#139656=CARTESIAN_POINT ( 'NONE',  ( 8.994519915287490619, 28.92564299267944250, 4.000000000000000000 ) ) ;
#139658=CARTESIAN_POINT ( 'NONE',  ( 26.58838509405149964, 22.22500000000000497, 4.777194822843814137 ) ) ;
#139659=DIRECTION ( 'NONE',  ( 0.7071067811865486830, -0.7071067811865464625, -0.000000000000000000 ) ) ;
#139660=VERTEX_POINT ( 'NONE', #42655 ) ;
#139662=VERTEX_POINT ( 'NONE', #7834 ) ;
#139665=CARTESIAN_POINT ( 'NONE',  ( 39.09667064187382124, -2.240707523384260824, 15.26439735382761498 ) ) ;
#139666=EDGE_CURVE ( 'NONE', #43833, #330, #52079, .T. ) ;
#139668=CARTESIAN_POINT ( 'NONE',  ( -5.576721541936426441, 11.25929247661560950, 17.85071094206586295 ) ) ;
#139670=VERTEX_POINT ( 'NONE', #96253 ) ;
#139671=CARTESIAN_POINT ( 'NONE',  ( -28.25154412867557951, -11.24070752338417201, 10.39518518046015849 ) ) ;
#139672=ADVANCED_FACE ( 'NONE', ( #64379 ), #128911, .T. ) ;
#139673=DIRECTION ( 'NONE',  ( -0.7071067811865486830, -0.7071067811865464625, 0.000000000000000000 ) ) ;
#139675=PLANE ( 'NONE',  #76910 ) ;
#139677=VECTOR ( 'NONE', #86433, 1000.000000000000227 ) ;
#139678=CARTESIAN_POINT ( 'NONE',  ( 22.49999999999984368, -1.695981523266237634, 4.571483868317931964 ) ) ;
#139679=VERTEX_POINT ( 'NONE', #97714 ) ;
#139680=EDGE_CURVE ( 'NONE', #121606, #127483, #108550, .T. ) ;
#139682=CARTESIAN_POINT ( 'NONE',  ( 14.68342038867201360, -6.740707523384212863, 11.88629033278120950 ) ) ;
#139683=AXIS2_PLACEMENT_3D ( 'NONE', #58970, #103123, #122726 ) ;
#139684=DIRECTION ( 'NONE',  ( -0.7071067811865486830, -0.7071067811865464625, -0.000000000000000000 ) ) ;
#139686=CARTESIAN_POINT ( 'NONE',  ( -34.92500000000001137, -22.22500000000000142, 4.500000000000000888 ) ) ;
#139688=DIRECTION ( 'NONE',  ( -1.000000000000000000, 0.000000000000000000, 0.000000000000000000 ) ) ;
#139690=LINE ( 'NONE', #15000, #41880 ) ;
#139692=EDGE_CURVE ( 'NONE', #99513, #10686, #107851, .T. ) ;
#139693=CARTESIAN_POINT ( 'NONE',  ( 45.29974487139158867, -27.71228299555237840, 4.000000000000000000 ) ) ;
#139694=VERTEX_POINT ( 'NONE', #86137 ) ;
#139696=DIRECTION ( 'NONE',  ( 0.3543493200069163240, 0.000000000000000000, 0.9351131265310288487 ) ) ;
#139697=FACE_OUTER_BOUND ( 'NONE', #57970, .T. ) ;
#139699=EDGE_LOOP ( 'NONE', ( #80672, #27312, #127508, #73696 ) ) ;
#139702=VECTOR ( 'NONE', #95201, 1000.000000000000000 ) ;
#139704=LINE ( 'NONE', #107029, #36426 ) ;
#139705=LINE ( 'NONE', #16433, #22286 ) ;
#139706=EDGE_LOOP ( 'NONE', ( #114778, #33524, #36148, #96951 ) ) ;
#139707=DIRECTION ( 'NONE',  ( 0.7071067811865487940, 0.7071067811865463515, 0.000000000000000000 ) ) ;
#139708=CARTESIAN_POINT ( 'NONE',  ( 34.92499999999998295, -14.66188269655938825, 18.97781875781096161 ) ) ;
#139709=VECTOR ( 'NONE', #138148, 1000.000000000000000 ) ;
#139710=VERTEX_POINT ( 'NONE', #107155 ) ;
#139711=ADVANCED_FACE ( 'NONE', ( #98435 ), #142656, .F. ) ;
#139712=VECTOR ( 'NONE', #90682, 999.9999999999998863 ) ;
#139713=DIRECTION ( 'NONE',  ( 0.6830127018922181881, 0.6830127018922202975, -0.2588190451025214056 ) ) ;
#139714=CARTESIAN_POINT ( 'NONE',  ( 24.55388970886357569, 5.485012786255876627, 4.000000000000000000 ) ) ;
#139716=VERTEX_POINT ( 'NONE', #54949 ) ;
#139718=VERTEX_POINT ( 'NONE', #43349 ) ;
#139719=ADVANCED_FACE ( 'NONE', ( #63691 ), #87560, .F. ) ;
#139720=ADVANCED_FACE ( 'NONE', ( #117999 ), #130365, .F. ) ;
#139721=DIRECTION ( 'NONE',  ( -0.7071067811865486830, -0.7071067811865464625, 0.000000000000000000 ) ) ;
#139722=DIRECTION ( 'NONE',  ( -0.7071067811865486830, -0.7071067811865464625, 0.000000000000000000 ) ) ;
#139723=CARTESIAN_POINT ( 'NONE',  ( -29.18650864602343731, -15.74070752338412049, 8.904080028139009784 ) ) ;
#139724=DIRECTION ( 'NONE',  ( 0.7071067811865486830, -0.7071067811865464625, -0.000000000000000000 ) ) ;
#139726=AXIS2_PLACEMENT_3D ( 'NONE', #36641, #25768, #133139 ) ;
#139727=PLANE ( 'NONE',  #65118 ) ;
#139732=ORIENTED_EDGE ( 'NONE', *, *, #67741, .T. ) ;
#139734=ORIENTED_EDGE ( 'NONE', *, *, #114521, .F. ) ;
#139735=AXIS2_PLACEMENT_3D ( 'NONE', #68710, #121621, #90443 ) ;
#139738=CARTESIAN_POINT ( 'NONE',  ( -9.328169399223462221, -9.740707523384187994, 4.000000000000000000 ) ) ;
#139739=ORIENTED_EDGE ( 'NONE', *, *, #99190, .T. ) ;
#139740=DIRECTION ( 'NONE',  ( 0.000000000000000000, 0.000000000000000000, -1.000000000000000000 ) ) ;
#139741=CARTESIAN_POINT ( 'NONE',  ( 48.48921356237309510, -27.52281430457089328, 5.000000000000000000 ) ) ;
#139743=AXIS2_PLACEMENT_3D ( 'NONE', #135261, #58440, #136643 ) ;
#139744=LINE ( 'NONE', #104192, #32918 ) ;
#139745=ORIENTED_EDGE ( 'NONE', *, *, #78473, .T. ) ;
#139748=CARTESIAN_POINT ( 'NONE',  ( -18.18398860626898994, 28.73617430169800002, 5.000000000000000000 ) ) ;
#139749=VERTEX_POINT ( 'NONE', #56408 ) ;
#139750=CARTESIAN_POINT ( 'NONE',  ( -72.48921356237309510, -27.52281430457106026, 5.000000000000000000 ) ) ;
#139755=ORIENTED_EDGE ( 'NONE', *, *, #86896, .T. ) ;
#139756=CARTESIAN_POINT ( 'NONE',  ( -33.29974487139158867, -27.71228299555229313, 4.000000000000000000 ) ) ;
#139758=VECTOR ( 'NONE', #98377, 1000.000000000000000 ) ;
#139761=CARTESIAN_POINT ( 'NONE',  ( 44.99451991528749772, 28.92564299267969474, 4.000000000000000000 ) ) ;
#139763=LINE ( 'NONE', #40445, #7340 ) ;
#139764=CARTESIAN_POINT ( 'NONE',  ( 20.99999999999985789, 13.93112307739204248, 4.000000000000000000 ) ) ;
#139765=FACE_OUTER_BOUND ( 'NONE', #124214, .T. ) ;
#139766=ADVANCED_FACE ( 'NONE', ( #133231 ), #91154, .F. ) ;
#139768=AXIS2_PLACEMENT_3D ( 'NONE', #137575, #28816, #62161 ) ;
#139771=VERTEX_POINT ( 'NONE', #124470 ) ;
#139773=CARTESIAN_POINT ( 'NONE',  ( -66.48921356237309510, -27.52281430457101763, 5.000000000000000000 ) ) ;
#139774=VERTEX_POINT ( 'NONE', #36057 ) ;
#139776=ORIENTED_EDGE ( 'NONE', *, *, #78486, .F. ) ;
#139777=VERTEX_POINT ( 'NONE', #132533 ) ;
#139778=DIRECTION ( 'NONE',  ( 0.6830127018922180770, -0.6830127018922204085, -0.2588190451025213501 ) ) ;
#139779=CARTESIAN_POINT ( 'NONE',  ( 5.816011393731002066, 28.73617430169783304, 5.000000000000000000 ) ) ;
#139782=EDGE_CURVE ( 'NONE', #121662, #9178, #12829, .T. ) ;
#139783=DIRECTION ( 'NONE',  ( 0.3543493200069163240, -0.000000000000000000, -0.9351131265310288487 ) ) ;
#139786=ORIENTED_EDGE ( 'NONE', *, *, #87087, .F. ) ;
#139787=VECTOR ( 'NONE', #70230, 1000.000000000000000 ) ;
#139789=AXIS2_PLACEMENT_3D ( 'NONE', #55842, #98599, #142829 ) ;
#139791=DIRECTION ( 'NONE',  ( -0.6830127018922181881, 0.6830127018922202975, -0.2588190451025214056 ) ) ;
#139792=DIRECTION ( 'NONE',  ( -0.7071067811865486830, 0.7071067811865464625, 0.000000000000000000 ) ) ;
#139794=ORIENTED_EDGE ( 'NONE', *, *, #14014, .T. ) ;
#139795=ORIENTED_EDGE ( 'NONE', *, *, #75742, .T. ) ;
#139797=CARTESIAN_POINT ( 'NONE',  ( 15.29974487139158867, -27.71228299555216879, 4.000000000000000000 ) ) ;
#139798=EDGE_CURVE ( 'NONE', #97591, #26803, #24437, .T. ) ;
#139799=PLANE ( 'NONE',  #126047 ) ;
#139800=DIRECTION ( 'NONE',  ( -0.7071067811865486830, 0.7071067811865463515, 0.000000000000000000 ) ) ;
#139801=AXIS2_PLACEMENT_3D ( 'NONE', #64699, #129215, #85708 ) ;
#139802=DIRECTION ( 'NONE',  ( -0.7071067811865486830, -0.7071067811865464625, 0.000000000000000000 ) ) ;
#139804=LINE ( 'NONE', #73804, #139162 ) ;
#139805=DIRECTION ( 'NONE',  ( 1.000000000000000000, 0.000000000000000000, 0.000000000000000000 ) ) ;
#139806=VECTOR ( 'NONE', #63310, 1000.000000000000000 ) ;
#139808=CARTESIAN_POINT ( 'NONE',  ( -19.49999999999986500, -1.592773361805389865, -6.492772025301184691 ) ) ;
#139810=VERTEX_POINT ( 'NONE', #13536 ) ;
#139811=DIRECTION ( 'NONE',  ( 0.7071067811865487940, 0.7071067811865463515, -0.000000000000000000 ) ) ;
#139812=ADVANCED_FACE ( 'NONE', ( #46967 ), #135375, .F. ) ;
#139814=EDGE_LOOP ( 'NONE', ( #56356, #117584, #41941, #57665 ) ) ;
#139815=( BOUNDED_CURVE ( )  B_SPLINE_CURVE ( 3, ( #127172, #5380, #38053, #71387 ),
 .UNSPECIFIED., .F., .T. ) 
 B_SPLINE_CURVE_WITH_KNOTS ( ( 4, 4 ),
 ( 5.143245962375964986, 6.645403452391247079 ),
 .UNSPECIFIED. ) 
 CURVE ( )  GEOMETRIC_REPRESENTATION_ITEM ( )  RATIONAL_B_SPLINE_CURVE ( ( 1.000000000000000000, 0.8206354192515239454, 0.8206354192515239454, 1.000000000000000000 ) ) 
 REPRESENTATION_ITEM ( '' )  );
#139816=AXIS2_PLACEMENT_3D ( 'NONE', #30672, #19058, #140817 ) ;
#139817=CARTESIAN_POINT ( 'NONE',  ( 36.48921356237310221, -27.52281430457080802, 5.000000000000000000 ) ) ;
#139818=CARTESIAN_POINT ( 'NONE',  ( -7.828169399223476432, 12.75929247661558996, 4.000000000000000000 ) ) ;
#139819=ORIENTED_EDGE ( 'NONE', *, *, #44396, .F. ) ;
#139821=EDGE_CURVE ( 'NONE', #68994, #1274, #59948, .T. ) ;
#139822=ADVANCED_FACE ( 'NONE', ( #104110 ), #81713, .F. ) ;
#139823=ORIENTED_EDGE ( 'NONE', *, *, #137527, .F. ) ;
#139824=DIRECTION ( 'NONE',  ( -0.6830127018922181881, 0.6830127018922202975, -0.2588190451025214056 ) ) ;
#139826=ORIENTED_EDGE ( 'NONE', *, *, #35661, .T. ) ;
#139827=VECTOR ( 'NONE', #19543, 1000.000000000000000 ) ;
#139829=EDGE_CURVE ( 'NONE', #112546, #98060, #4773, .T. ) ;
#139831=DIRECTION ( 'NONE',  ( 0.6830127018922180770, -0.6830127018922204085, -0.2588190451025213501 ) ) ;
#139832=CIRCLE ( 'NONE', #5442, 5.968999999999998529 ) ;
#139833=CARTESIAN_POINT ( 'NONE',  ( 34.92499999999998295, 17.81665438641027777, 4.500000000000000888 ) ) ;
#139834=DIRECTION ( 'NONE',  ( 0.6830127018922181881, 0.6830127018922202975, -0.2588190451025214056 ) ) ;
#139835=DIRECTION ( 'NONE',  ( 0.7071067811865487940, 0.7071067811865463515, 0.000000000000000000 ) ) ;
#139836=LINE ( 'NONE', #116619, #124704 ) ;
#139840=PLANE ( 'NONE',  #113818 ) ;
#139841=DIRECTION ( 'NONE',  ( -0.000000000000000000, 0.3543493200069153248, 0.9351131265310292928 ) ) ;
#139843=ORIENTED_EDGE ( 'NONE', *, *, #35640, .T. ) ;
#139845=PLANE ( 'NONE',  #4972 ) ;
#139846=ORIENTED_EDGE ( 'NONE', *, *, #13305, .T. ) ;
#139848=DIRECTION ( 'NONE',  ( 0.7071067811865487940, -0.7071067811865463515, 0.000000000000000000 ) ) ;
#139850=DIRECTION ( 'NONE',  ( -0.000000000000000000, 0.000000000000000000, 1.000000000000000000 ) ) ;
#139851=ORIENTED_EDGE ( 'NONE', *, *, #90930, .F. ) ;
#139852=CARTESIAN_POINT ( 'NONE',  ( -26.99999999999980815, -13.97847968911263017, -0.1324546996127407283 ) ) ;
#139855=VERTEX_POINT ( 'NONE', #117143 ) ;
#139856=CYLINDRICAL_SURFACE ( 'NONE', #136921, 0.5000000000000004441 ) ;
#139857=CARTESIAN_POINT ( 'NONE',  ( -30.18398860626900060, 28.73617430169808173, 5.000000000000000000 ) ) ;
#139858=DIRECTION ( 'NONE',  ( 1.000000000000000000, 0.000000000000000000, 0.000000000000000000 ) ) ;
#139859=DIRECTION ( 'NONE',  ( 0.7071067811865487940, -0.7071067811865463515, 0.000000000000000000 ) ) ;
#139860=DIRECTION ( 'NONE',  ( -0.7071067811865486830, -0.7071067811865464625, -0.000000000000000000 ) ) ;
#139863=ORIENTED_EDGE ( 'NONE', *, *, #67548, .T. ) ;
#139864=VERTEX_POINT ( 'NONE', #125913 ) ;
#139866=VECTOR ( 'NONE', #55417, 1000.000000000000227 ) ;
#139867=ORIENTED_EDGE ( 'NONE', *, *, #103953, .F. ) ;
#139869=DIRECTION ( 'NONE',  ( -0.7071067811865486830, -0.7071067811865464625, 0.000000000000000000 ) ) ;
#139870=ORIENTED_EDGE ( 'NONE', *, *, #127197, .F. ) ;
#139871=LINE ( 'NONE', #40547, #123168 ) ;
#139872=DIRECTION ( 'NONE',  ( -0.000000000000000000, 0.3543493200069153248, 0.9351131265310292928 ) ) ;
#139875=ORIENTED_EDGE ( 'NONE', *, *, #118068, .F. ) ;
#139876=CARTESIAN_POINT ( 'NONE',  ( 17.27718569542927796, -21.72500000000000142, 5.000000000000000000 ) ) ;
#139878=DIRECTION ( 'NONE',  ( -0.7071067811865486830, -0.7071067811865464625, -0.000000000000000000 ) ) ;
#139879=CARTESIAN_POINT ( 'NONE',  ( -26.67183060077628198, -12.74070752338415602, 4.000000000000000000 ) ) ;
#139880=LINE ( 'NONE', #29905, #76337 ) ;
#139881=ORIENTED_EDGE ( 'NONE', *, *, #59136, .F. ) ;
#139882=EDGE_LOOP ( 'NONE', ( #140676, #29486, #124197, #15324 ) ) ;
#139883=EDGE_CURVE ( 'NONE', #38066, #135973, #116452, .T. ) ;
#139884=VERTEX_POINT ( 'NONE', #38893 ) ;
#139885=DIRECTION ( 'NONE',  ( -0.7071067811865487940, 0.7071067811865463515, -0.000000000000000000 ) ) ;
#139886=ADVANCED_FACE ( 'NONE', ( #70829 ), #15659, .F. ) ;
#139887=CARTESIAN_POINT ( 'NONE',  ( 18.45983838949729261, 18.75929247661552779, 8.305906642995529054 ) ) ;
#139889=VECTOR ( 'NONE', #11302, 1000.000000000000000 ) ;
#139890=CARTESIAN_POINT ( 'NONE',  ( 12.70710678118646619, 14.25929247661557220, 5.000000000000000000 ) ) ;
#139891=AXIS2_PLACEMENT_3D ( 'NONE', #121958, #32861, #66895 ) ;
#139892=ORIENTED_EDGE ( 'NONE', *, *, #48773, .F. ) ;
#139893=EDGE_CURVE ( 'NONE', #126064, #16024, #83860, .T. ) ;
#139894=VERTEX_POINT ( 'NONE', #48339 ) ;
#139895=CARTESIAN_POINT ( 'NONE',  ( -42.48921356237308800, -27.52281430457085065, 5.000000000000000000 ) ) ;
#139896=ORIENTED_EDGE ( 'NONE', *, *, #59276, .F. ) ;
#139897=ORIENTED_EDGE ( 'NONE', *, *, #131117, .F. ) ;
#139898=EDGE_CURVE ( 'NONE', #86742, #131471, #47669, .T. ) ;
#139899=LINE ( 'NONE', #95643, #49493 ) ;
#139900=ORIENTED_EDGE ( 'NONE', *, *, #114923, .F. ) ;
#139901=VECTOR ( 'NONE', #26021, 1000.000000000000000 ) ;
#139902=CARTESIAN_POINT ( 'NONE',  ( 5.700255128608413102, -27.71228299555201957, 4.000000000000000000 ) ) ;
#139903=AXIS2_PLACEMENT_3D ( 'NONE', #93677, #137189, #84251 ) ;
#139904=DIRECTION ( 'NONE',  ( 0.7071067811865487940, 0.7071067811865463515, -0.000000000000000000 ) ) ;
#139905=DIRECTION ( 'NONE',  ( 0.7071067811865486830, -0.7071067811865464625, -0.000000000000000000 ) ) ;
#139906=EDGE_CURVE ( 'NONE', #64904, #6181, #92529, .T. ) ;
#139907=PLANE ( 'NONE',  #46708 ) ;
#139908=EDGE_LOOP ( 'NONE', ( #91825, #56034, #9289, #7927 ) ) ;
#139909=LINE ( 'NONE', #110092, #34845 ) ;
#139910=FACE_BOUND ( 'NONE', #116925, .T. ) ;
#139911=VECTOR ( 'NONE', #31357, 1000.000000000000114 ) ;
#139912=ORIENTED_EDGE ( 'NONE', *, *, #75771, .T. ) ;
#139916=EDGE_LOOP ( 'NONE', ( #123540, #16205, #42294, #79539 ) ) ;
#139917=LINE ( 'NONE', #40595, #27369 ) ;
#139918=ORIENTED_EDGE ( 'NONE', *, *, #80690, .F. ) ;
#139920=ORIENTED_EDGE ( 'NONE', *, *, #25981, .F. ) ;
#139923=LINE ( 'NONE', #1334, #54461 ) ;
#139924=AXIS2_PLACEMENT_3D ( 'NONE', #73092, #109792, #105660 ) ;
#139925=DIRECTION ( 'NONE',  ( -0.000000000000000000, 0.3543493200069153248, 0.9351131265310292928 ) ) ;
#139926=LINE ( 'NONE', #83388, #114336 ) ;
#139927=DIRECTION ( 'NONE',  ( -0.7071067811865486830, 0.7071067811865464625, 0.000000000000000000 ) ) ;
#139929=ADVANCED_FACE ( 'NONE', ( #138207 ), #50489, .T. ) ;
#139930=CARTESIAN_POINT ( 'NONE',  ( 30.18398860626900060, 28.73617430169808173, 5.000000000000000000 ) ) ;
#139931=CARTESIAN_POINT ( 'NONE',  ( -48.48921356237309510, -27.52281430457089328, 5.000000000000000000 ) ) ;
#139932=FACE_OUTER_BOUND ( 'NONE', #140339, .T. ) ;
#139934=EDGE_CURVE ( 'NONE', #92161, #71721, #6212, .T. ) ;
#139935=DIRECTION ( 'NONE',  ( -0.7071067811865486830, -0.7071067811865464625, 0.000000000000000000 ) ) ;
#139936=CARTESIAN_POINT ( 'NONE',  ( -16.49999999999988987, 16.18958161055400780, -11.56426086740815151 ) ) ;
#139937=CARTESIAN_POINT ( 'NONE',  ( 10.37176554955608943, -8.240707523384196875, 11.38925528200750215 ) ) ;
#139938=VERTEX_POINT ( 'NONE', #39633 ) ;
#139939=EDGE_LOOP ( 'NONE', ( #87903, #64764, #127240, #75112 ) ) ;
#139941=ORIENTED_EDGE ( 'NONE', *, *, #66692, .T. ) ;
#139943=ORIENTED_EDGE ( 'NONE', *, *, #59863, .F. ) ;
#139944=ADVANCED_FACE ( 'NONE', ( #28746 ), #72989, .F. ) ;
#139945=ORIENTED_EDGE ( 'NONE', *, *, #68920, .F. ) ;
#139946=LINE ( 'NONE', #53638, #86187 ) ;
#139948=ADVANCED_FACE ( 'NONE', ( #70140 ), #53324, .F. ) ;
#139949=EDGE_CURVE ( 'NONE', #92353, #133121, #106252, .T. ) ;
#139950=DIRECTION ( 'NONE',  ( -0.7071067811865486830, -0.7071067811865464625, 0.000000000000000000 ) ) ;
#139952=CARTESIAN_POINT ( 'NONE',  ( -48.48921356237309510, -27.52281430457089328, 5.000000000000000000 ) ) ;
#139954=LINE ( 'NONE', #61680, #113864 ) ;
#139955=DIRECTION ( 'NONE',  ( -0.000000000000000000, -0.000000000000000000, 1.000000000000000000 ) ) ;
#139957=ORIENTED_EDGE ( 'NONE', *, *, #9258, .T. ) ;
#139959=ADVANCED_FACE ( 'NONE', ( #20696 ), #85235, .F. ) ;
#139960=CARTESIAN_POINT ( 'NONE',  ( -54.18398860626899705, 28.73617430169825226, 5.000000000000000000 ) ) ;
#139962=LINE ( 'NONE', #115279, #136840 ) ;
#139963=ORIENTED_EDGE ( 'NONE', *, *, #13968, .T. ) ;
#139964=ORIENTED_EDGE ( 'NONE', *, *, #49954, .T. ) ;
#139967=CARTESIAN_POINT ( 'NONE',  ( -15.79289321881334551, -8.240707523384191546, 5.000000000000000000 ) ) ;
#139968=DIRECTION ( 'NONE',  ( -0.3543493200069162685, -0.000000000000000000, -0.9351131265310288487 ) ) ;
#139970=FACE_OUTER_BOUND ( 'NONE', #90668, .T. ) ;
#139972=VECTOR ( 'NONE', #73932, 1000.000000000000000 ) ;
#139973=ORIENTED_EDGE ( 'NONE', *, *, #62518, .F. ) ;
#139975=DIRECTION ( 'NONE',  ( -0.000000000000000000, -0.3543493200069152693, 0.9351131265310292928 ) ) ;
#139976=DIRECTION ( 'NONE',  ( 2.781805975412905274E-17, -0.3543493200069152138, 0.9351131265310292928 ) ) ;
#139977=EDGE_LOOP ( 'NONE', ( #3798, #129770, #125131, #122587 ) ) ;
#139980=ORIENTED_EDGE ( 'NONE', *, *, #119303, .F. ) ;
#139981=LINE ( 'NONE', #65282, #41769 ) ;
#139982=VERTEX_POINT ( 'NONE', #129458 ) ;
#139983=VERTEX_POINT ( 'NONE', #7671 ) ;
#139984=DIRECTION ( 'NONE',  ( 0.7071067811865487940, 0.7071067811865463515, -0.000000000000000000 ) ) ;
#139985=LINE ( 'NONE', #40660, #133999 ) ;
#139986=EDGE_CURVE ( 'NONE', #96522, #26845, #130200, .T. ) ;
#139988=VERTEX_POINT ( 'NONE', #85965 ) ;
#139989=DIRECTION ( 'NONE',  ( 0.3543493200069162685, -0.000000000000000000, -0.9351131265310288487 ) ) ;
#139992=EDGE_CURVE ( 'NONE', #44425, #43477, #62810, .T. ) ;
#139993=AXIS2_PLACEMENT_3D ( 'NONE', #61584, #108577, #41951 ) ;
#139994=DIRECTION ( 'NONE',  ( -0.7071067811865486830, -0.7071067811865464625, -0.000000000000000000 ) ) ;
#139995=AXIS2_PLACEMENT_3D ( 'NONE', #126423, #69222, #60501 ) ;
#139997=DIRECTION ( 'NONE',  ( 0.7071067811865487940, -0.7071067811865463515, 0.000000000000000000 ) ) ;
#139998=DIRECTION ( 'NONE',  ( 0.6830127018922181881, 0.6830127018922202975, -0.2588190451025214056 ) ) ;
#139999=DIRECTION ( 'NONE',  ( -0.6830127018922180770, -0.6830127018922204085, -0.2588190451025213501 ) ) ;
#140000=LINE ( 'NONE', #84202, #58350 ) ;
#140001=CARTESIAN_POINT ( 'NONE',  ( 0.000000000000000000, 0.000000000000000000, 5.000000000000000000 ) ) ;
#140003=ORIENTED_EDGE ( 'NONE', *, *, #42781, .T. ) ;
#140004=EDGE_LOOP ( 'NONE', ( #137168, #129329, #103149, #48849 ) ) ;
#140005=ORIENTED_EDGE ( 'NONE', *, *, #102774, .F. ) ;
#140008=AXIS2_PLACEMENT_3D ( 'NONE', #51899, #96761, #95374 ) ;
#140009=ORIENTED_EDGE ( 'NONE', *, *, #58177, .T. ) ;
#140010=ORIENTED_EDGE ( 'NONE', *, *, #55768, .F. ) ;
#140011=CARTESIAN_POINT ( 'NONE',  ( 48.29974487139158867, -27.71228299555239971, 4.000000000000000000 ) ) ;
#140012=CARTESIAN_POINT ( 'NONE',  ( -13.17183060077638324, -8.240707523384200428, 4.000000000000000000 ) ) ;
#140014=CARTESIAN_POINT ( 'NONE',  ( 33.18398860626899705, 28.73617430169810305, 5.000000000000000000 ) ) ;
#140015=CARTESIAN_POINT ( 'NONE',  ( -9.489213562373095101, -27.52281430457062328, 5.000000000000000000 ) ) ;
#140016=CARTESIAN_POINT ( 'NONE',  ( -5.816011393731002066, 28.73617430169783304, 5.000000000000000000 ) ) ;
#140017=DIRECTION ( 'NONE',  ( 0.3543493200069162685, -0.000000000000000000, -0.9351131265310288487 ) ) ;
#140019=ORIENTED_EDGE ( 'NONE', *, *, #90832, .F. ) ;
#140020=CARTESIAN_POINT ( 'NONE',  ( 22.49999999999984723, -16.53360074219757081, 5.000000000000000000 ) ) ;
#140021=DIRECTION ( 'NONE',  ( -0.3543493200069162685, -0.000000000000000000, -0.9351131265310288487 ) ) ;
#140022=DIRECTION ( 'NONE',  ( -0.000000000000000000, -0.3543493200069152693, 0.9351131265310292928 ) ) ;
#140023=DIRECTION ( 'NONE',  ( 0.7071067811865487940, 0.7071067811865463515, -0.000000000000000000 ) ) ;
#140024=CARTESIAN_POINT ( 'NONE',  ( -12.79289321881336861, -8.240707523384198652, 5.000000000000000000 ) ) ;
#140025=FACE_OUTER_BOUND ( 'NONE', #108614, .T. ) ;
#140027=DIRECTION ( 'NONE',  ( 0.3543493200069162685, -0.000000000000000000, -0.9351131265310288487 ) ) ;
#140028=VECTOR ( 'NONE', #44134, 1000.000000000000227 ) ;
#140030=ORIENTED_EDGE ( 'NONE', *, *, #41528, .F. ) ;
#140031=ORIENTED_EDGE ( 'NONE', *, *, #2054, .F. ) ;
#140032=VECTOR ( 'NONE', #21004, 1000.000000000000000 ) ;
#140034=ORIENTED_EDGE ( 'NONE', *, *, #5824, .T. ) ;
#140036=DIRECTION ( 'NONE',  ( -0.000000000000000000, 0.3543493200069153248, 0.9351131265310292928 ) ) ;
#140037=DIRECTION ( 'NONE',  ( 0.7071067811865486830, -0.7071067811865464625, -0.000000000000000000 ) ) ;
#140038=CARTESIAN_POINT ( 'NONE',  ( 34.92499999999998295, -19.19990548397263552, 4.759050581649326261 ) ) ;
#140039=PLANE ( 'NONE',  #118633 ) ;
#140044=CARTESIAN_POINT ( 'NONE',  ( 23.99451991528749062, 28.92564299267954908, 4.000000000000000000 ) ) ;
#140045=ORIENTED_EDGE ( 'NONE', *, *, #128014, .T. ) ;
#140046=CARTESIAN_POINT ( 'NONE',  ( 9.995075227787999950, -5.240707523384225297, 12.38332538355493817 ) ) ;
#140047=DIRECTION ( 'NONE',  ( 0.7071067811865486830, -0.7071067811865464625, -0.000000000000000000 ) ) ;
#140049=EDGE_CURVE ( 'NONE', #112107, #132154, #51207, .T. ) ;
#140050=DIRECTION ( 'NONE',  ( -0.7071067811865486830, -0.7071067811865464625, 0.000000000000000000 ) ) ;
#140051=VERTEX_POINT ( 'NONE', #74395 ) ;
#140053=EDGE_CURVE ( 'NONE', #22619, #65995, #96797, .T. ) ;
#140054=VERTEX_POINT ( 'NONE', #141046 ) ;
#140055=FACE_OUTER_BOUND ( 'NONE', #135006, .T. ) ;
#140056=CARTESIAN_POINT ( 'NONE',  ( 21.18398860626899349, 28.73617430169802134, 5.000000000000000000 ) ) ;
#140057=CARTESIAN_POINT ( 'NONE',  ( 11.20666063542144286, 21.75929247661549937, 4.998822639870701856 ) ) ;
#140058=CARTESIAN_POINT ( 'NONE',  ( 21.18398860626899349, 28.73617430169802134, 5.000000000000000000 ) ) ;
#140059=ADVANCED_FACE ( 'NONE', ( #75119 ), #54092, .F. ) ;
#140060=EDGE_CURVE ( 'NONE', #58311, #10476, #19975, .T. ) ;
#140061=ADVANCED_FACE ( 'NONE', ( #17821 ), #108383, .F. ) ;
#140064=EDGE_CURVE ( 'NONE', #86178, #56732, #97542, .T. ) ;
#140065=CARTESIAN_POINT ( 'NONE',  ( 30.29974487139158867, -27.71228299555227537, 4.000000000000000000 ) ) ;
#140067=EDGE_LOOP ( 'NONE', ( #88327, #35820, #25303, #22793 ) ) ;
#140068=EDGE_LOOP ( 'NONE', ( #99094, #141717, #69771, #48046 ) ) ;
#140069=VECTOR ( 'NONE', #100521, 1000.000000000000227 ) ;
#140070=EDGE_CURVE ( 'NONE', #52608, #9115, #86697, .T. ) ;
#140071=CARTESIAN_POINT ( 'NONE',  ( -15.68879807097514956, -1.757674993583058898, 4.000000000000000000 ) ) ;
#140074=ORIENTED_EDGE ( 'NONE', *, *, #68724, .T. ) ;
#140077=ADVANCED_FACE ( 'NONE', ( #75817 ), #40347, .F. ) ;
#140079=FACE_BOUND ( 'NONE', #82416, .T. ) ;
#140080=VERTEX_POINT ( 'NONE', #9822 ) ;
#140081=LINE ( 'NONE', #64641, #138307 ) ;
#140083=ORIENTED_EDGE ( 'NONE', *, *, #71725, .T. ) ;
#140085=ORIENTED_EDGE ( 'NONE', *, *, #133868, .F. ) ;
#140086=EDGE_CURVE ( 'NONE', #114619, #74261, #142504, .T. ) ;
#140087=VERTEX_POINT ( 'NONE', #355 ) ;
#140088=PLANE ( 'NONE',  #128186 ) ;
#140089=ORIENTED_EDGE ( 'NONE', *, *, #53996, .T. ) ;
#140090=VECTOR ( 'NONE', #16418, 1000.000000000000227 ) ;
#140095=FACE_OUTER_BOUND ( 'NONE', #56102, .T. ) ;
#140096=ADVANCED_FACE ( 'NONE', ( #134481 ), #67078, .F. ) ;
#140099=EDGE_CURVE ( 'NONE', #64709, #4325, #120718, .T. ) ;
#140100=CARTESIAN_POINT ( 'NONE',  ( -17.20710678118642178, -11.24070752338416312, 5.000000000000000000 ) ) ;
#140101=VECTOR ( 'NONE', #65290, 1000.000000000000000 ) ;
#140103=DIRECTION ( 'NONE',  ( 0.7071067811865487940, 0.7071067811865463515, 0.000000000000000000 ) ) ;
#140104=EDGE_CURVE ( 'NONE', #125864, #41067, #77267, .T. ) ;
#140105=CARTESIAN_POINT ( 'NONE',  ( -22.77325839282152131, -11.24070752338416845, 18.24660765846977384 ) ) ;
#140107=ORIENTED_EDGE ( 'NONE', *, *, #33962, .F. ) ;
#140108=LINE ( 'NONE', #84990, #137594 ) ;
#140109=DIRECTION ( 'NONE',  ( 0.7071067811865487940, -0.7071067811865463515, 0.000000000000000000 ) ) ;
#140110=VERTEX_POINT ( 'NONE', #67827 ) ;
#140111=ADVANCED_FACE ( 'NONE', ( #88114 ), #99679, .F. ) ;
#140112=VERTEX_POINT ( 'NONE', #122872 ) ;
#140113=EDGE_LOOP ( 'NONE', ( #106700, #13883, #64991, #31845 ) ) ;
#140114=CARTESIAN_POINT ( 'NONE',  ( -1.641757024588595737, 15.75929247661555799, 19.34181609438699923 ) ) ;
#140115=DIRECTION ( 'NONE',  ( 0.6830127018922180770, -0.6830127018922204085, -0.2588190451025213501 ) ) ;
#140116=ORIENTED_EDGE ( 'NONE', *, *, #101254, .F. ) ;
#140117=CARTESIAN_POINT ( 'NONE',  ( -2.241399257802041856, 21.72499999999999432, 5.000000000000000000 ) ) ;
#140119=CARTESIAN_POINT ( 'NONE',  ( 39.18398860626899705, 28.73617430169814568, 5.000000000000000000 ) ) ;
#140120=AXIS2_PLACEMENT_3D ( 'NONE', #83616, #4522, #127826 ) ;
#140122=VECTOR ( 'NONE', #142607, 1000.000000000000000 ) ;
#140123=DIRECTION ( 'NONE',  ( 0.7071067811865487940, 0.7071067811865463515, 0.000000000000000000 ) ) ;
#140124=VERTEX_POINT ( 'NONE', #133070 ) ;
#140126=VECTOR ( 'NONE', #11485, 1000.000000000000000 ) ;
#140127=EDGE_CURVE ( 'NONE', #121270, #47360, #11955, .T. ) ;
#140128=LINE ( 'NONE', #118335, #72127 ) ;
#140129=CARTESIAN_POINT ( 'NONE',  ( 54.48921356237310221, -27.52281430457093236, 5.000000000000000000 ) ) ;
#140130=CARTESIAN_POINT ( 'NONE',  ( -14.81601139373099585, 28.73617430169776910, 5.000000000000000000 ) ) ;
#140131=ORIENTED_EDGE ( 'NONE', *, *, #71045, .F. ) ;
#140132=DIRECTION ( 'NONE',  ( 0.3543493200069162685, -0.000000000000000000, -0.9351131265310288487 ) ) ;
#140133=EDGE_LOOP ( 'NONE', ( #86467, #69289, #137042, #105348 ) ) ;
#140135=ADVANCED_FACE ( 'NONE', ( #13370 ), #24276, .F. ) ;
#140137=LINE ( 'NONE', #40811, #102744 ) ;
#140138=ORIENTED_EDGE ( 'NONE', *, *, #86153, .T. ) ;
#140139=DIRECTION ( 'NONE',  ( -0.6830127018922180770, -0.6830127018922204085, -0.2588190451025213501 ) ) ;
#140140=CARTESIAN_POINT ( 'NONE',  ( 26.67183060077628554, 8.259292476615632594, 4.000000000000000000 ) ) ;
#140144=CARTESIAN_POINT ( 'NONE',  ( 6.299744871391586898, -27.71228299555210484, 4.000000000000000000 ) ) ;
#140145=CARTESIAN_POINT ( 'NONE',  ( -25.17183060077629619, -2.240707523384257716, 4.000000000000000000 ) ) ;
#140146=LINE ( 'NONE', #16170, #14776 ) ;
#140147=CARTESIAN_POINT ( 'NONE',  ( -9.183988606268997046, 28.73617430169793607, 5.000000000000000000 ) ) ;
#140148=ORIENTED_EDGE ( 'NONE', *, *, #137503, .F. ) ;
#140150=DIRECTION ( 'NONE',  ( -0.7071067811865486830, -0.7071067811865464625, 0.000000000000000000 ) ) ;
#140151=LINE ( 'NONE', #42983, #62190 ) ;
#140153=DIRECTION ( 'NONE',  ( 0.7071067811865487940, 0.7071067811865463515, 0.000000000000000000 ) ) ;
#140154=EDGE_CURVE ( 'NONE', #111064, #70001, #132363, .T. ) ;
#140155=DIRECTION ( 'NONE',  ( -0.7071067811865487940, 0.7071067811865463515, -0.000000000000000000 ) ) ;
#140156=FACE_OUTER_BOUND ( 'NONE', #98801, .T. ) ;
#140157=ORIENTED_EDGE ( 'NONE', *, *, #27944, .T. ) ;
#140158=LINE ( 'NONE', #38695, #120510 ) ;
#140159=DIRECTION ( 'NONE',  ( 0.7071067811865487940, 0.7071067811865463515, 0.000000000000000000 ) ) ;
#140162=CARTESIAN_POINT ( 'NONE',  ( -19.05000000000000071, 3.174999999999997158, 4.000000000000000000 ) ) ;
#140165=EDGE_LOOP ( 'NONE', ( #77184, #112519, #9614, #112931 ) ) ;
#140166=VERTEX_POINT ( 'NONE', #1757 ) ;
#140167=CARTESIAN_POINT ( 'NONE',  ( -8.163471288734461595, 15.75929247661555976, 9.299976744542901130 ) ) ;
#140168=DIRECTION ( 'NONE',  ( -0.7071067811865486830, -0.7071067811865464625, 0.000000000000000000 ) ) ;
#140169=DIRECTION ( 'NONE',  ( 0.7071067811865487940, -0.7071067811865463515, 0.000000000000000000 ) ) ;
#140170=PLANE ( 'NONE',  #129925 ) ;
#140171=CARTESIAN_POINT ( 'NONE',  ( -30.79289321881324426, -8.240707523384196875, 5.000000000000000000 ) ) ;
#140173=LINE ( 'NONE', #63358, #70880 ) ;
#140174=ORIENTED_EDGE ( 'NONE', *, *, #68057, .T. ) ;
#140175=DIRECTION ( 'NONE',  ( -0.7071067811865486830, 0.7071067811865464625, 0.000000000000000000 ) ) ;
#140177=LINE ( 'NONE', #107530, #93507 ) ;
#140178=DIRECTION ( 'NONE',  ( -0.000000000000000000, 0.3543493200069153248, 0.9351131265310292928 ) ) ;
#140179=PLANE ( 'NONE',  #68213 ) ;
#140183=LINE ( 'NONE', #85074, #34557 ) ;
#140184=ORIENTED_EDGE ( 'NONE', *, *, #78750, .T. ) ;
#140185=ORIENTED_EDGE ( 'NONE', *, *, #9092, .T. ) ;
#140187=CARTESIAN_POINT ( 'NONE',  ( -2.207106781186525701, 3.759292476615680112, 5.000000000000000000 ) ) ;
#140188=CARTESIAN_POINT ( 'NONE',  ( -2.999999999999968026, -16.44781430457066662, 5.000000000000000000 ) ) ;
#140189=CARTESIAN_POINT ( 'NONE',  ( 14.51078643762690490, -27.52281430457045275, 5.000000000000000000 ) ) ;
#140190=ORIENTED_EDGE ( 'NONE', *, *, #47815, .T. ) ;
#140191=( BOUNDED_CURVE ( )  B_SPLINE_CURVE ( 3, ( #104098, #28734, #4760, #138920 ),
 .UNSPECIFIED., .F., .F. ) 
 B_SPLINE_CURVE_WITH_KNOTS ( ( 4, 4 ),
 ( 4.350170835173033268, 4.500739107949262241 ),
 .UNSPECIFIED. ) 
 CURVE ( )  GEOMETRIC_REPRESENTATION_ITEM ( )  RATIONAL_B_SPLINE_CURVE ( ( 1.000000000000000000, 0.9981116584018946414, 0.9981116584018946414, 1.000000000000000000 ) ) 
 REPRESENTATION_ITEM ( '' )  );
#140192=CARTESIAN_POINT ( 'NONE',  ( 66.18398860626901126, 28.73617430169833753, 5.000000000000000000 ) ) ;
#140193=VECTOR ( 'NONE', #64939, 1000.000000000000000 ) ;
#140195=EDGE_LOOP ( 'NONE', ( #99983, #84866, #108695, #49362 ) ) ;
#140196=ADVANCED_FACE ( 'NONE', ( #66370 ), #90984, .F. ) ;
#140198=ORIENTED_EDGE ( 'NONE', *, *, #15923, .T. ) ;
#140200=ORIENTED_EDGE ( 'NONE', *, *, #93924, .F. ) ;
#140201=DIRECTION ( 'NONE',  ( -0.7071067811865486830, -0.7071067811865464625, 0.000000000000000000 ) ) ;
#140202=CARTESIAN_POINT ( 'NONE',  ( -9.183988606268997046, 28.73617430169793607, 5.000000000000000000 ) ) ;
#140203=VERTEX_POINT ( 'NONE', #57647 ) ;
#140204=LINE ( 'NONE', #87958, #2541 ) ;
#140205=ADVANCED_FACE ( 'NONE', ( #77956 ), #122140, .F. ) ;
#140207=CARTESIAN_POINT ( 'NONE',  ( -30.18398860626900060, 28.73617430169808173, 5.000000000000000000 ) ) ;
#140208=ORIENTED_EDGE ( 'NONE', *, *, #106808, .T. ) ;
#140210=DIRECTION ( 'NONE',  ( 0.7071067811865486830, -0.7071067811865464625, -0.000000000000000000 ) ) ;
#140211=LINE ( 'NONE', #118438, #36885 ) ;
#140212=VECTOR ( 'NONE', #97569, 1000.000000000000000 ) ;
#140213=EDGE_CURVE ( 'NONE', #106288, #68187, #14428, .T. ) ;
#140215=EDGE_CURVE ( 'NONE', #37549, #101265, #98959, .T. ) ;
#140217=EDGE_CURVE ( 'NONE', #90401, #72522, #143200, .T. ) ;
#140218=VECTOR ( 'NONE', #43791, 1000.000000000000000 ) ;
#140221=PLANE ( 'NONE',  #37197 ) ;
#140223=DIRECTION ( 'NONE',  ( 1.000000000000000000, -0.000000000000000000, 0.000000000000000000 ) ) ;
#140224=DIRECTION ( 'NONE',  ( -0.000000000000000000, -0.3543493200069152693, 0.9351131265310292928 ) ) ;
#140225=EDGE_LOOP ( 'NONE', ( #70612, #56399, #15434, #94431 ) ) ;
#140227=AXIS2_PLACEMENT_3D ( 'NONE', #7078, #51360, #95552 ) ;
#140229=DIRECTION ( 'NONE',  ( -0.6830127018922180770, -0.6830127018922204085, -0.2588190451025213501 ) ) ;
#140230=DIRECTION ( 'NONE',  ( -0.7071067811865486830, -0.7071067811865464625, -0.000000000000000000 ) ) ;
#140231=VERTEX_POINT ( 'NONE', #7311 ) ;
#140232=EDGE_CURVE ( 'NONE', #93195, #58856, #80116, .T. ) ;
#140234=CARTESIAN_POINT ( 'NONE',  ( 34.45011844616451668, 13.51628081163735828, 5.000000000000000888 ) ) ;
#140235=ORIENTED_EDGE ( 'NONE', *, *, #117157, .F. ) ;
#140236=CARTESIAN_POINT ( 'NONE',  ( 34.92499999999998295, 0.5846064065779636998, -3.200354092940492112 ) ) ;
#140237=EDGE_CURVE ( 'NONE', #17447, #125425, #107358, .T. ) ;
#140238=CARTESIAN_POINT ( 'NONE',  ( -34.47516574401891631, -14.97193265888402181, 4.998110765256835286 ) ) ;
#140239=FACE_BOUND ( 'NONE', #35300, .T. ) ;
#140242=LINE ( 'NONE', #9702, #41062 ) ;
#140243=DIRECTION ( 'NONE',  ( -0.000000000000000000, 0.000000000000000000, 1.000000000000000000 ) ) ;
#140244=EDGE_LOOP ( 'NONE', ( #59335, #67905, #141887, #10513 ) ) ;
#140245=EDGE_CURVE ( 'NONE', #118125, #18521, #51577, .T. ) ;
#140246=LINE ( 'NONE', #61989, #90335 ) ;
#140248=ORIENTED_EDGE ( 'NONE', *, *, #1693, .F. ) ;
#140249=ORIENTED_EDGE ( 'NONE', *, *, #45704, .T. ) ;
#140251=ORIENTED_EDGE ( 'NONE', *, *, #110411, .T. ) ;
#140252=DIRECTION ( 'NONE',  ( -0.6830127018922180770, -0.6830127018922204085, -0.2588190451025213501 ) ) ;
#140253=DIRECTION ( 'NONE',  ( -0.6830127018922180770, -0.6830127018922204085, -0.2588190451025213501 ) ) ;
#140254=PLANE ( 'NONE',  #51334 ) ;
#140255=DIRECTION ( 'NONE',  ( -0.7071067811865486830, -0.7071067811865464625, -0.000000000000000000 ) ) ;
#140256=ADVANCED_FACE ( 'NONE', ( #96446 ), #18920, .T. ) ;
#140258=DIRECTION ( 'NONE',  ( -0.7071067811865486830, -0.7071067811865464625, 0.000000000000000000 ) ) ;
#140259=CARTESIAN_POINT ( 'NONE',  ( 5.671830600776438303, 5.259292476615662792, 4.000000000000000000 ) ) ;
#140260=EDGE_CURVE ( 'NONE', #39036, #83246, #52264, .T. ) ;
#140262=CARTESIAN_POINT ( 'NONE',  ( 45.29974487139158867, -27.71228299555237840, 4.000000000000000000 ) ) ;
#140263=PLANE ( 'NONE',  #86296 ) ;
#140265=LINE ( 'NONE', #8971, #28743 ) ;
#140266=EDGE_CURVE ( 'NONE', #34599, #79126, #50141, .T. ) ;
#140267=PLANE ( 'NONE',  #35157 ) ;
#140268=ORIENTED_EDGE ( 'NONE', *, *, #116414, .F. ) ;
#140269=VERTEX_POINT ( 'NONE', #113409 ) ;
#140270=ORIENTED_EDGE ( 'NONE', *, *, #99267, .F. ) ;
#140272=VERTEX_POINT ( 'NONE', #58389 ) ;
#140273=DIRECTION ( 'NONE',  ( 0.7071067811865487940, 0.7071067811865463515, -0.000000000000000000 ) ) ;
#140274=VECTOR ( 'NONE', #130419, 1000.000000000000227 ) ;
#140277=ORIENTED_EDGE ( 'NONE', *, *, #124732, .T. ) ;
#140278=AXIS2_PLACEMENT_3D ( 'NONE', #71395, #115556, #135925 ) ;
#140279=ADVANCED_FACE ( 'NONE', ( #102572 ), #3216, .F. ) ;
#140282=PLANE ( 'NONE',  #132126 ) ;
#140283=PLANE ( 'NONE',  #47542 ) ;
#140284=LINE ( 'NONE', #107638, #23980 ) ;
#140287=DIRECTION ( 'NONE',  ( -0.7071067811865486830, -0.7071067811865464625, -0.000000000000000000 ) ) ;
#140288=ORIENTED_EDGE ( 'NONE', *, *, #80164, .T. ) ;
#140289=LINE ( 'NONE', #87343, #43533 ) ;
#140290=ORIENTED_EDGE ( 'NONE', *, *, #104590, .T. ) ;
#140291=ORIENTED_EDGE ( 'NONE', *, *, #114260, .F. ) ;
#140292=VERTEX_POINT ( 'NONE', #140691 ) ;
#140294=PLANE ( 'NONE',  #102789 ) ;
#140295=PLANE ( 'NONE',  #141876 ) ;
#140296=CARTESIAN_POINT ( 'NONE',  ( 34.49999999999976552, 0.05432934483094861711, 4.994342998332161443 ) ) ;
#140297=DIRECTION ( 'NONE',  ( 0.7071067811865487940, 0.7071067811865463515, -0.000000000000000000 ) ) ;
#140298=EDGE_CURVE ( 'NONE', #16022, #8423, #126958, .T. ) ;
#140299=PLANE ( 'NONE',  #50621 ) ;
#140300=EDGE_LOOP ( 'NONE', ( #45647, #94715, #111722, #24788 ) ) ;
#140301=CARTESIAN_POINT ( 'NONE',  ( -60.18398860626900415, 28.73617430169829490, 5.000000000000000000 ) ) ;
#140302=ORIENTED_EDGE ( 'NONE', *, *, #23752, .T. ) ;
#140303=FACE_OUTER_BOUND ( 'NONE', #52360, .T. ) ;
#140304=VECTOR ( 'NONE', #85992, 1000.000000000000000 ) ;
#140306=CARTESIAN_POINT ( 'NONE',  ( 12.81349135397630867, -15.74070752338412404, 8.904080028138910308 ) ) ;
#140307=EDGE_LOOP ( 'NONE', ( #110998, #113141, #102209, #88588 ) ) ;
#140308=PLANE ( 'NONE',  #131699 ) ;
#140309=CARTESIAN_POINT ( 'NONE',  ( 29.20710678118634718, 12.75929247661558996, 5.000000000000000000 ) ) ;
#140310=ADVANCED_FACE ( 'NONE', ( #61063 ), #71917, .F. ) ;
#140311=EDGE_LOOP ( 'NONE', ( #12199, #67496, #9330, #74406 ) ) ;
#140312=EDGE_LOOP ( 'NONE', ( #128527, #36058, #119582, #132135 ) ) ;
#140314=PLANE ( 'NONE',  #88233 ) ;
#140315=UNCERTAINTY_MEASURE_WITH_UNIT (LENGTH_MEASURE( 1.000000000000000082E-05 ), #121660, 'distance_accuracy_value', 'NONE');
#140316=CARTESIAN_POINT ( 'NONE',  ( 69.29974487139159578, -27.71228299555254537, 4.000000000000000000 ) ) ;
#140317=VECTOR ( 'NONE', #105888, 1000.000000000000000 ) ;
#140318=LINE ( 'NONE', #41004, #68315 ) ;
#140320=ADVANCED_FACE ( 'NONE', ( #105217 ), #5874, .F. ) ;
#140321=CARTESIAN_POINT ( 'NONE',  ( -0.2997448713915885632, -27.71228299555206220, 4.000000000000000000 ) ) ;
#140322=CARTESIAN_POINT ( 'NONE',  ( 34.92499999999998295, -21.72500000000000142, 5.000000000000000000 ) ) ;
#140323=EDGE_CURVE ( 'NONE', #14903, #99523, #84895, .T. ) ;
#140324=LINE ( 'NONE', #41009, #104285 ) ;
#140325=DIRECTION ( 'NONE',  ( 0.7071067811865487940, 0.7071067811865463515, 0.000000000000000000 ) ) ;
#140327=PLANE ( 'NONE',  #69650 ) ;
#140328=ORIENTED_EDGE ( 'NONE', *, *, #133809, .T. ) ;
#140329=LINE ( 'NONE', #121419, #36270 ) ;
#140330=FACE_OUTER_BOUND ( 'NONE', #11192, .T. ) ;
#140331=ORIENTED_EDGE ( 'NONE', *, *, #121138, .T. ) ;
#140332=DIRECTION ( 'NONE',  ( 0.3543493200069163240, 0.000000000000000000, 0.9351131265310288487 ) ) ;
#140333=CARTESIAN_POINT ( 'NONE',  ( -34.92500000000001137, -18.28150956279557704, 4.759050581649344025 ) ) ;
#140334=ORIENTED_EDGE ( 'NONE', *, *, #140730, .T. ) ;
#140336=FACE_OUTER_BOUND ( 'NONE', #40594, .T. ) ;
#140337=DIRECTION ( 'NONE',  ( -0.7071067811865486830, -0.7071067811865464625, -0.000000000000000000 ) ) ;
#140339=EDGE_LOOP ( 'NONE', ( #52945, #24930, #136386, #23592 ) ) ;
#140342=LINE ( 'NONE', #96793, #119352 ) ;
#140344=CARTESIAN_POINT ( 'NONE',  ( -51.48921356237309510, -27.52281430457091460, 5.000000000000000000 ) ) ;
#140345=CARTESIAN_POINT ( 'NONE',  ( 0.7928932188134528714, 9.759292476615627265, 5.000000000000000000 ) ) ;
#140346=ORIENTED_EDGE ( 'NONE', *, *, #6647, .F. ) ;
#140347=DIRECTION ( 'NONE',  ( 0.6830127018922180770, -0.6830127018922204085, -0.2588190451025213501 ) ) ;
#140348=PLANE ( 'NONE',  #80939 ) ;
#140350=VECTOR ( 'NONE', #45535, 1000.000000000000000 ) ;
#140351=DIRECTION ( 'NONE',  ( 0.000000000000000000, -1.000000000000000000, 0.000000000000000000 ) ) ;
#140352=EDGE_LOOP ( 'NONE', ( #76268, #8055, #27591, #52893 ) ) ;
#140353=DIRECTION ( 'NONE',  ( 0.7071067811865487940, 0.7071067811865463515, 0.000000000000000000 ) ) ;
#140354=EDGE_LOOP ( 'NONE', ( #36374, #78267, #86262, #65917 ) ) ;
#140356=CARTESIAN_POINT ( 'NONE',  ( 60.48921356237309510, -27.52281430457097500, 5.000000000000000000 ) ) ;
#140357=VECTOR ( 'NONE', #117650, 999.9999999999998863 ) ;
#140358=CARTESIAN_POINT ( 'NONE',  ( -28.49999999999980460, 11.52377502935400955, -1.522421517564018112 ) ) ;
#140359=ORIENTED_EDGE ( 'NONE', *, *, #19563, .T. ) ;
#140360=DIRECTION ( 'NONE',  ( 1.000000000000000000, 0.000000000000000000, 0.000000000000000000 ) ) ;
#140361=FACE_OUTER_BOUND ( 'NONE', #49497, .T. ) ;
#140362=PLANE ( 'NONE',  #43971 ) ;
#140363=EDGE_CURVE ( 'NONE', #71971, #13935, #129107, .T. ) ;
#140364=CARTESIAN_POINT ( 'NONE',  ( -34.92500000000001137, 22.22500000000000142, 4.500000000000000888 ) ) ;
#140365=ORIENTED_EDGE ( 'NONE', *, *, #44603, .F. ) ;
#140366=CARTESIAN_POINT ( 'NONE',  ( 3.198522738312878477, 22.22500000000000142, -9.446427897663703277 ) ) ;
#140368=( BOUNDED_CURVE ( )  B_SPLINE_CURVE ( 3, ( #117280, #73808, #29570, #140478 ),
 .UNSPECIFIED., .F., .F. ) 
 B_SPLINE_CURVE_WITH_KNOTS ( ( 4, 4 ),
 ( 5.043186909253408956, 5.074607125596339863 ),
 .UNSPECIFIED. ) 
 CURVE ( )  GEOMETRIC_REPRESENTATION_ITEM ( )  RATIONAL_B_SPLINE_CURVE ( ( 1.000000000000000000, 0.9999177325257868620, 0.9999177325257868620, 1.000000000000000000 ) ) 
 REPRESENTATION_ITEM ( '' )  );
#140369=LINE ( 'NONE', #61437, #21511 ) ;
#140370=ORIENTED_EDGE ( 'NONE', *, *, #118277, .T. ) ;
#140371=VECTOR ( 'NONE', #119199, 1000.000000000000000 ) ;
#140373=EDGE_CURVE ( 'NONE', #26996, #99025, #40003, .T. ) ;
#140375=VERTEX_POINT ( 'NONE', #128415 ) ;
#140378=CARTESIAN_POINT ( 'NONE',  ( -18.98911971346038285, -22.02621442084247860, 4.990779571109222879 ) ) ;
#140379=EDGE_CURVE ( 'NONE', #73261, #89868, #21785, .T. ) ;
#140380=CARTESIAN_POINT ( 'NONE',  ( 22.49999999999985434, -10.91253812416064228, 4.000000000000000000 ) ) ;
#140382=ORIENTED_EDGE ( 'NONE', *, *, #67677, .F. ) ;
#140383=ADVANCED_FACE ( 'NONE', ( #99317 ), #10180, .F. ) ;
#140384=CARTESIAN_POINT ( 'NONE',  ( 42.18398860626899705, 28.73617430169816700, 5.000000000000000000 ) ) ;
#140386=ORIENTED_EDGE ( 'NONE', *, *, #16156, .T. ) ;
#140387=VECTOR ( 'NONE', #6276, 1000.000000000000000 ) ;
#140388=EDGE_CURVE ( 'NONE', #91909, #68198, #59756, .T. ) ;
#140389=CARTESIAN_POINT ( 'NONE',  ( 29.99999999999979039, -11.35517001088069300, -1.126524801160039724 ) ) ;
#140390=DIRECTION ( 'NONE',  ( 0.000000000000000000, 1.000000000000000000, -0.000000000000000000 ) ) ;
#140391=DIRECTION ( 'NONE',  ( -0.7071067811865486830, -0.7071067811865464625, -0.000000000000000000 ) ) ;
#140392=ORIENTED_EDGE ( 'NONE', *, *, #102968, .F. ) ;
#140394=ADVANCED_FACE ( 'NONE', ( #120336 ), #97923, .T. ) ;
#140395=VECTOR ( 'NONE', #102778, 999.9999999999998863 ) ;
#140397=DIRECTION ( 'NONE',  ( 0.6830127018922181881, 0.6830127018922202975, -0.2588190451025214056 ) ) ;
#140398=CARTESIAN_POINT ( 'NONE',  ( 8.816011393731004731, 28.73617430169781173, 5.000000000000000000 ) ) ;
#140399=CARTESIAN_POINT ( 'NONE',  ( -20.99999999999985789, 19.55218569542897100, 5.000000000000000000 ) ) ;
#140404=AXIS2_PLACEMENT_3D ( 'NONE', #124342, #93142, #25010 ) ;
#140405=CARTESIAN_POINT ( 'NONE',  ( 8.999999999999943157, -1.447814304570811617, 5.000000000000000000 ) ) ;
#140407=EDGE_LOOP ( 'NONE', ( #125939, #91272, #129070, #81273 ) ) ;
#140408=VECTOR ( 'NONE', #108785, 1000.000000000000000 ) ;
#140409=ORIENTED_EDGE ( 'NONE', *, *, #13989, .T. ) ;
#140410=VERTEX_POINT ( 'NONE', #33417 ) ;
#140411=VERTEX_POINT ( 'NONE', #142160 ) ;
#140412=VECTOR ( 'NONE', #11387, 1000.000000000000000 ) ;
#140413=LINE ( 'NONE', #87475, #116515 ) ;
#140414=ORIENTED_EDGE ( 'NONE', *, *, #131427, .F. ) ;
#140416=CARTESIAN_POINT ( 'NONE',  ( 83.99451991528748351, 28.92564299267996830, 4.000000000000000000 ) ) ;
#140417=CARTESIAN_POINT ( 'NONE',  ( 42.18398860626899705, 28.73617430169816700, 5.000000000000000000 ) ) ;
#140418=EDGE_CURVE ( 'NONE', #30830, #63481, #100070, .T. ) ;
#140419=CARTESIAN_POINT ( 'NONE',  ( -72.29974487139158157, -27.71228299555256669, 4.000000000000000000 ) ) ;
#140420=DIRECTION ( 'NONE',  ( 0.7071067811865486830, -0.7071067811865464625, -0.000000000000000000 ) ) ;
#140422=PLANE ( 'NONE',  #93505 ) ;
#140424=ORIENTED_EDGE ( 'NONE', *, *, #79908, .F. ) ;
#140425=CARTESIAN_POINT ( 'NONE',  ( -25.00051279177633390, 3.647752439586037454, 4.157751055492734160 ) ) ;
#140426=EDGE_LOOP ( 'NONE', ( #82713, #123853, #123183, #22763 ) ) ;
#140428=ORIENTED_EDGE ( 'NONE', *, *, #50861, .F. ) ;
#140430=VERTEX_POINT ( 'NONE', #20331 ) ;
#140431=ORIENTED_EDGE ( 'NONE', *, *, #120997, .T. ) ;
#140432=EDGE_CURVE ( 'NONE', #87956, #105448, #85593, .T. ) ;
#140433=DIRECTION ( 'NONE',  ( 1.000000000000000000, 0.000000000000000000, 0.000000000000000000 ) ) ;
#140434=VECTOR ( 'NONE', #130493, 1000.000000000000000 ) ;
#140435=CARTESIAN_POINT ( 'NONE',  ( 27.18398860626900060, 28.73617430169806042, 5.000000000000000000 ) ) ;
#140437=DIRECTION ( 'NONE',  ( 0.7071067811865486830, -0.7071067811865464625, -0.000000000000000000 ) ) ;
#140438=EDGE_CURVE ( 'NONE', #108363, #50134, #64575, .T. ) ;
#140439=DIRECTION ( 'NONE',  ( -0.7071067811865486830, -0.7071067811865464625, 0.000000000000000000 ) ) ;
#140440=PLANE ( 'NONE',  #92655 ) ;
#140443=DIRECTION ( 'NONE',  ( 0.7071067811865486830, -0.7071067811865464625, -0.000000000000000000 ) ) ;
#140444=PLANE ( 'NONE',  #38195 ) ;
#140446=CARTESIAN_POINT ( 'NONE',  ( -26.99451991528749417, 28.92564299267956685, 4.000000000000000000 ) ) ;
#140447=EDGE_CURVE ( 'NONE', #36187, #135322, #88487, .T. ) ;
#140448=ORIENTED_EDGE ( 'NONE', *, *, #48182, .F. ) ;
#140449=ORIENTED_EDGE ( 'NONE', *, *, #45766, .T. ) ;
#140450=ORIENTED_EDGE ( 'NONE', *, *, #83139, .F. ) ;
#140451=AXIS2_PLACEMENT_3D ( 'NONE', #31243, #51570, #95763 ) ;
#140455=VECTOR ( 'NONE', #105788, 1000.000000000000000 ) ;
#140456=EDGE_CURVE ( 'NONE', #30730, #99209, #19637, .T. ) ;
#140457=DIRECTION ( 'NONE',  ( -0.6830127018922180770, -0.6830127018922204085, -0.2588190451025213501 ) ) ;
#140458=EDGE_LOOP ( 'NONE', ( #4513, #31819, #71424, #123715 ) ) ;
#140460=ORIENTED_EDGE ( 'NONE', *, *, #69458, .F. ) ;
#140463=DIRECTION ( 'NONE',  ( 0.7071067811865487940, 0.7071067811865463515, 0.000000000000000000 ) ) ;
#140464=ORIENTED_EDGE ( 'NONE', *, *, #127417, .T. ) ;
#140465=ORIENTED_EDGE ( 'NONE', *, *, #75911, .F. ) ;
#140466=VECTOR ( 'NONE', #138033, 1000.000000000000000 ) ;
#140467=ORIENTED_EDGE ( 'NONE', *, *, #108227, .F. ) ;
#140468=DIRECTION ( 'NONE',  ( -0.7071067811865487940, 0.7071067811865463515, 0.000000000000000000 ) ) ;
#140469=LINE ( 'NONE', #85368, #106610 ) ;
#140470=DIRECTION ( 'NONE',  ( -0.6830127018922181881, 0.6830127018922202975, -0.2588190451025214056 ) ) ;
#140471=CARTESIAN_POINT ( 'NONE',  ( -14.58838509405158135, 22.22500000000000142, 4.777194822843813249 ) ) ;
#140472=LINE ( 'NONE', #61536, #6531 ) ;
#140473=ADVANCED_FACE ( 'NONE', ( #53721 ), #42846, .T. ) ;
#140474=CARTESIAN_POINT ( 'NONE',  ( 34.49999999999975842, -13.53574439159937093, 4.994342998332162331 ) ) ;
#140475=DIRECTION ( 'NONE',  ( 0.6830127018922180770, -0.6830127018922204085, -0.2588190451025213501 ) ) ;
#140476=EDGE_CURVE ( 'NONE', #23492, #128513, #65323, .T. ) ;
#140478=CARTESIAN_POINT ( 'NONE',  ( -12.72281430457050710, -21.72500000000000142, 5.000000000000000000 ) ) ;
#140479=ORIENTED_EDGE ( 'NONE', *, *, #21487, .T. ) ;
#140480=FACE_OUTER_BOUND ( 'NONE', #37413, .T. ) ;
#140481=CARTESIAN_POINT ( 'NONE',  ( 39.18398860626899705, 28.73617430169814568, 5.000000000000000000 ) ) ;
#140482=EDGE_LOOP ( 'NONE', ( #86947, #90246, #122703, #91020 ) ) ;
#140486=ADVANCED_FACE ( 'NONE', ( #121086 ), #109506, .F. ) ;
#140487=LINE ( 'NONE', #54245, #76960 ) ;
#140489=EDGE_LOOP ( 'NONE', ( #48990, #121380, #55026, #16628 ) ) ;
#140491=ORIENTED_EDGE ( 'NONE', *, *, #132746, .F. ) ;
#140492=VECTOR ( 'NONE', #140390, 1000.000000000000000 ) ;
#140494=VECTOR ( 'NONE', #76218, 1000.000000000000000 ) ;
#140496=AXIS2_PLACEMENT_3D ( 'NONE', #14296, #91849, #111465 ) ;
#140498=DIRECTION ( 'NONE',  ( -0.000000000000000000, -0.3543493200069152693, 0.9351131265310292928 ) ) ;
#140499=CARTESIAN_POINT ( 'NONE',  ( 34.49999999999976552, 18.05432934483075513, 4.994342998332162331 ) ) ;
#140500=CARTESIAN_POINT ( 'NONE',  ( -15.18398860626900237, 28.73617430169797871, 5.000000000000000000 ) ) ;
#140501=DIRECTION ( 'NONE',  ( 0.7071067811865487940, 0.7071067811865463515, 0.000000000000000000 ) ) ;
#140503=CARTESIAN_POINT ( 'NONE',  ( 17.99451991528748351, 28.92564299267950645, 4.000000000000000000 ) ) ;
#140507=CARTESIAN_POINT ( 'NONE',  ( -72.48921356237309510, -27.52281430457106026, 5.000000000000000000 ) ) ;
#140508=LINE ( 'NONE', #137687, #131209 ) ;
#140510=EDGE_CURVE ( 'NONE', #126872, #117172, #10869, .T. ) ;
#140513=EDGE_LOOP ( 'NONE', ( #92213, #13905, #137336, #18913 ) ) ;
#140514=DIRECTION ( 'NONE',  ( -0.7071067811865486830, -0.7071067811865464625, -0.000000000000000000 ) ) ;
#140515=DIRECTION ( 'NONE',  ( 1.000000000000000000, 0.000000000000000000, 0.000000000000000000 ) ) ;
#140516=CARTESIAN_POINT ( 'NONE',  ( 35.91508676806215306, -12.74070752338415957, 18.74364270924362685 ) ) ;
#140518=CARTESIAN_POINT ( 'NONE',  ( -28.49999999999979750, -4.533600742197692490, 5.000000000000000000 ) ) ;
#140520=LINE ( 'NONE', #41212, #122973 ) ;
#140522=LINE ( 'NONE', #18002, #84516 ) ;
#140523=ORIENTED_EDGE ( 'NONE', *, *, #66274, .F. ) ;
#140524=CARTESIAN_POINT ( 'NONE',  ( -60.18398860626900415, 28.73617430169829490, 5.000000000000000000 ) ) ;
#140525=AXIS2_PLACEMENT_3D ( 'NONE', #38472, #83410, #115261 ) ;
#140526=CARTESIAN_POINT ( 'NONE',  ( 0.000000000000000000, 15.45873954670184780, -0.03131636524294264395 ) ) ;
#140527=DIRECTION ( 'NONE',  ( -0.7071067811865487940, 0.7071067811865463515, -0.000000000000000000 ) ) ;
#140528=FACE_OUTER_BOUND ( 'NONE', #86659, .T. ) ;
#140529=PLANE ( 'NONE',  #93843 ) ;
#140530=LINE ( 'NONE', #129655, #30634 ) ;
#140531=ORIENTED_EDGE ( 'NONE', *, *, #31623, .F. ) ;
#140532=ORIENTED_EDGE ( 'NONE', *, *, #48078, .T. ) ;
#140533=EDGE_LOOP ( 'NONE', ( #122001, #68117, #34979, #7918 ) ) ;
#140534=ADVANCED_FACE ( 'NONE', ( #132728 ), #113059, .F. ) ;
#140536=VECTOR ( 'NONE', #95113, 1000.000000000000000 ) ;
#140537=ORIENTED_EDGE ( 'NONE', *, *, #34063, .T. ) ;
#140538=ADVANCED_FACE ( 'NONE', ( #68196 ), #111656, .F. ) ;
#140540=AXIS2_PLACEMENT_3D ( 'NONE', #54294, #32518, #120933 ) ;
#140541=DIRECTION ( 'NONE',  ( 0.7071067811865487940, 0.7071067811865463515, -0.000000000000000000 ) ) ;
#140542=ORIENTED_EDGE ( 'NONE', *, *, #104357, .T. ) ;
#140543=EDGE_CURVE ( 'NONE', #7434, #70301, #35560, .T. ) ;
#140545=DIRECTION ( 'NONE',  ( 0.7071067811865487940, 0.7071067811865463515, -0.000000000000000000 ) ) ;
#140546=LINE ( 'NONE', #128963, #72125 ) ;
#140548=EDGE_LOOP ( 'NONE', ( #109423, #6257, #112080, #29366 ) ) ;
#140550=FACE_OUTER_BOUND ( 'NONE', #64494, .T. ) ;
#140552=CARTESIAN_POINT ( 'NONE',  ( -24.00548008471250938, 28.92564299267921513, 4.000000000000000000 ) ) ;
#140553=DIRECTION ( 'NONE',  ( -0.6830127018922181881, 0.6830127018922202975, -0.2588190451025214056 ) ) ;
#140554=EDGE_LOOP ( 'NONE', ( #37756, #77794, #4698, #44348 ) ) ;
#140555=ORIENTED_EDGE ( 'NONE', *, *, #80027, .F. ) ;
#140556=ADVANCED_FACE ( 'NONE', ( #3565 ), #14478, .T. ) ;
#140557=VECTOR ( 'NONE', #113663, 1000.000000000000227 ) ;
#140558=ORIENTED_EDGE ( 'NONE', *, *, #136296, .F. ) ;
#140559=DIRECTION ( 'NONE',  ( -0.3543493200069162685, -0.000000000000000000, -0.9351131265310288487 ) ) ;
#140560=ADVANCED_FACE ( 'NONE', ( #13026 ), #57303, .F. ) ;
#140561=DIRECTION ( 'NONE',  ( -0.7071067811865486830, 0.7071067811865464625, 0.000000000000000000 ) ) ;
#140564=EDGE_CURVE ( 'NONE', #89344, #137750, #143135, .T. ) ;
#140565=EDGE_LOOP ( 'NONE', ( #135621, #110772, #18522, #75632 ) ) ;
#140566=AXIS2_PLACEMENT_3D ( 'NONE', #118285, #76238, #42196 ) ;
#140567=ORIENTED_EDGE ( 'NONE', *, *, #74786, .F. ) ;
#140568=DIRECTION ( 'NONE',  ( -0.3543493200069163240, 0.000000000000000000, -0.9351131265310288487 ) ) ;
#140569=ORIENTED_EDGE ( 'NONE', *, *, #26988, .F. ) ;
#140570=ORIENTED_EDGE ( 'NONE', *, *, #82971, .F. ) ;
#140571=EDGE_CURVE ( 'NONE', #12215, #31122, #59444, .T. ) ;
#140573=ORIENTED_EDGE ( 'NONE', *, *, #85879, .T. ) ;
#140574=CARTESIAN_POINT ( 'NONE',  ( 2.999999999999981792, 4.931123077392134846, 4.000000000000000000 ) ) ;
#140575=DIRECTION ( 'NONE',  ( 0.7071067811865487940, 0.7071067811865463515, -0.000000000000000000 ) ) ;
#140576=EDGE_CURVE ( 'NONE', #33542, #36959, #114483, .T. ) ;
#140579=VERTEX_POINT ( 'NONE', #91351 ) ;
#140580=DIRECTION ( 'NONE',  ( 0.7071067811865486830, -0.7071067811865464625, -0.000000000000000000 ) ) ;
#140581=VECTOR ( 'NONE', #96314, 1000.000000000000000 ) ;
#140582=CARTESIAN_POINT ( 'NONE',  ( 8.510786437626906675, -27.52281430457049183, 5.000000000000000000 ) ) ;
#140583=VERTEX_POINT ( 'NONE', #125392 ) ;
#140585=CARTESIAN_POINT ( 'NONE',  ( -25.49999999999982236, 21.43112307739196254, 4.000000000000000000 ) ) ;
#140588=FACE_OUTER_BOUND ( 'NONE', #56504, .T. ) ;
#140589=ORIENTED_EDGE ( 'NONE', *, *, #1908, .F. ) ;
#140590=ORIENTED_EDGE ( 'NONE', *, *, #100954, .F. ) ;
#140591=VECTOR ( 'NONE', #56987, 999.9999999999998863 ) ;
#140592=VERTEX_POINT ( 'NONE', #45015 ) ;
#140593=AXIS2_PLACEMENT_3D ( 'NONE', #18413, #117728, #108272 ) ;
#140594=EDGE_CURVE ( 'NONE', #70558, #16196, #79063, .T. ) ;
#140595=VECTOR ( 'NONE', #40027, 1000.000000000000000 ) ;
#140598=CARTESIAN_POINT ( 'NONE',  ( -13.41009064519824179, 9.759292476615621936, 11.28811694763775542 ) ) ;
#140600=CARTESIAN_POINT ( 'NONE',  ( 7.499999999999947597, 19.39370406404968605, 1.459788787078186489 ) ) ;
#140601=CARTESIAN_POINT ( 'NONE',  ( -4.786780966966382778, 12.75929247661558996, 10.29404684609034071 ) ) ;
#140602=DIRECTION ( 'NONE',  ( 0.6830127018922181881, 0.6830127018922202975, -0.2588190451025214056 ) ) ;
#140603=AXIS2_PLACEMENT_3D ( 'NONE', #50524, #38228, #58605 ) ;
#140604=CARTESIAN_POINT ( 'NONE',  ( -2.708222910169498565, -15.74070752338411694, 19.73771281079097051 ) ) ;
#140605=FACE_OUTER_BOUND ( 'NONE', #68958, .T. ) ;
#140606=CARTESIAN_POINT ( 'NONE',  ( -34.49999999999975842, -11.94567065516892690, 4.994342998332167660 ) ) ;
#140607=CARTESIAN_POINT ( 'NONE',  ( 26.99999999999981881, -6.412538124160691133, 4.000000000000000000 ) ) ;
#140608=EDGE_CURVE ( 'NONE', #97802, #130638, #23178, .T. ) ;
#140609=ORIENTED_EDGE ( 'NONE', *, *, #64287, .T. ) ;
#140610=ORIENTED_EDGE ( 'NONE', *, *, #90905, .T. ) ;
#140614=ORIENTED_EDGE ( 'NONE', *, *, #80357, .T. ) ;
#140616=ORIENTED_EDGE ( 'NONE', *, *, #29406, .F. ) ;
#140617=DIRECTION ( 'NONE',  ( 1.000000000000000000, 0.000000000000000000, 0.000000000000000000 ) ) ;
#140619=ADVANCED_FACE ( 'NONE', ( #135560 ), #69604, .F. ) ;
#140620=PLANE ( 'NONE',  #113353 ) ;
#140622=VECTOR ( 'NONE', #69302, 999.9999999999998863 ) ;
#140624=ORIENTED_EDGE ( 'NONE', *, *, #88206, .T. ) ;
#140625=CARTESIAN_POINT ( 'NONE',  ( -11.51078643762690490, -27.52281430457047406, 5.000000000000000000 ) ) ;
#140626=CARTESIAN_POINT ( 'NONE',  ( -10.99806943317894437, -22.22500000000000142, 4.500000000000000888 ) ) ;
#140627=VECTOR ( 'NONE', #116590, 1000.000000000000000 ) ;
#140629=VERTEX_POINT ( 'NONE', #13732 ) ;
#140631=LINE ( 'NONE', #3841, #66815 ) ;
#140632=DIRECTION ( 'NONE',  ( 1.000000000000000000, 0.000000000000000000, 0.000000000000000000 ) ) ;
#140634=ORIENTED_EDGE ( 'NONE', *, *, #43812, .F. ) ;
#140636=CARTESIAN_POINT ( 'NONE',  ( 0.000000000000000000, 0.000000000000000000, 5.000000000000000000 ) ) ;
#140637=ORIENTED_EDGE ( 'NONE', *, *, #15161, .T. ) ;
#140638=VECTOR ( 'NONE', #43935, 1000.000000000000000 ) ;
#140639=CARTESIAN_POINT ( 'NONE',  ( 33.71230993966005229, -21.73547319004781286, 4.999917730833663754 ) ) ;
#140640=CARTESIAN_POINT ( 'NONE',  ( 53.99451991528749062, 28.92564299267975869, 4.000000000000000000 ) ) ;
#140641=LINE ( 'NONE', #85539, #14526 ) ;
#140642=LINE ( 'NONE', #129056, #873 ) ;
#140643=ORIENTED_EDGE ( 'NONE', *, *, #128680, .T. ) ;
#140644=CARTESIAN_POINT ( 'NONE',  ( 9.459838389497344124, 18.75929247661553489, 8.305906642995505962 ) ) ;
#140645=EDGE_CURVE ( 'NONE', #65778, #72974, #136245, .T. ) ;
#140646=DIRECTION ( 'NONE',  ( 0.7071067811865486830, -0.7071067811865464625, -0.000000000000000000 ) ) ;
#140647=CARTESIAN_POINT ( 'NONE',  ( 18.18398860626898994, 28.73617430169800002, 5.000000000000000000 ) ) ;
#140648=ORIENTED_EDGE ( 'NONE', *, *, #133188, .T. ) ;
#140649=DIRECTION ( 'NONE',  ( 0.7071067811865487940, -0.7071067811865463515, 0.000000000000000000 ) ) ;
#140651=ORIENTED_EDGE ( 'NONE', *, *, #78441, .F. ) ;
#140652=ADVANCED_FACE ( 'NONE', ( #58021 ), #68886, .T. ) ;
#140653=CARTESIAN_POINT ( 'NONE',  ( -34.92500000000001137, -2.993876922608041724, 4.000000000000000000 ) ) ;
#140654=EDGE_LOOP ( 'NONE', ( #10714, #19088, #104323, #90734 ) ) ;
#140656=EDGE_CURVE ( 'NONE', #54563, #116840, #25340, .T. ) ;
#140658=DIRECTION ( 'NONE',  ( 1.000000000000000000, 0.000000000000000000, 0.000000000000000000 ) ) ;
#140659=VERTEX_POINT ( 'NONE', #34106 ) ;
#140664=VECTOR ( 'NONE', #80890, 1000.000000000000000 ) ;
#140665=EDGE_CURVE ( 'NONE', #100474, #31073, #118024, .T. ) ;
#140668=DIRECTION ( 'NONE',  ( 0.6830127018922181881, 0.6830127018922202975, -0.2588190451025214056 ) ) ;
#140669=DIRECTION ( 'NONE',  ( -0.3543493200069163240, -0.000000000000000000, -0.9351131265310288487 ) ) ;
#140670=DIRECTION ( 'NONE',  ( 0.7071067811865487940, 0.7071067811865463515, 0.000000000000000000 ) ) ;
#140671=DIRECTION ( 'NONE',  ( 0.7071067811865487940, 0.7071067811865463515, 0.000000000000000000 ) ) ;
#140672=CARTESIAN_POINT ( 'NONE',  ( -2.816011393730999401, 28.73617430169785436, 5.000000000000000000 ) ) ;
#140673=CARTESIAN_POINT ( 'NONE',  ( 8.700255128608413102, -27.71228299555199825, 4.000000000000000000 ) ) ;
#140674=CARTESIAN_POINT ( 'NONE',  ( -25.49999999999982592, -14.56887692260765377, 4.000000000000000000 ) ) ;
#140675=DIRECTION ( 'NONE',  ( -0.7071067811865487940, 0.7071067811865463515, -0.000000000000000000 ) ) ;
#140676=ORIENTED_EDGE ( 'NONE', *, *, #115020, .F. ) ;
#140677=EDGE_CURVE ( 'NONE', #121970, #21922, #72473, .T. ) ;
#140678=ORIENTED_EDGE ( 'NONE', *, *, #58177, .F. ) ;
#140679=ORIENTED_EDGE ( 'NONE', *, *, #122335, .T. ) ;
#140683=ORIENTED_EDGE ( 'NONE', *, *, #134660, .F. ) ;
#140684=ORIENTED_EDGE ( 'NONE', *, *, #103262, .T. ) ;
#140687=ORIENTED_EDGE ( 'NONE', *, *, #87283, .F. ) ;
#140688=AXIS2_PLACEMENT_3D ( 'NONE', #1704, #99615, #111957 ) ;
#140690=CARTESIAN_POINT ( 'NONE',  ( 37.03163515922168614, 2.259292476615694323, 13.77329220150646094 ) ) ;
#140691=CARTESIAN_POINT ( 'NONE',  ( 10.82816939922345156, -20.24070752338408141, 4.000000000000000000 ) ) ;
#140692=CARTESIAN_POINT ( 'NONE',  ( 20.67183060077632462, -21.74070752338406365, 4.000000000000000000 ) ) ;
#140694=ORIENTED_EDGE ( 'NONE', *, *, #15290, .T. ) ;
#140695=CARTESIAN_POINT ( 'NONE',  ( -28.49999999999979750, 6.052185695429105117, 5.000000000000000000 ) ) ;
#140697=AXIS2_PLACEMENT_3D ( 'NONE', #68779, #24525, #69490 ) ;
#140699=DIRECTION ( 'NONE',  ( -0.7071067811865487940, 0.7071067811865463515, 0.000000000000000000 ) ) ;
#140701=VECTOR ( 'NONE', #105972, 1000.000000000000227 ) ;
#140703=PLANE ( 'NONE',  #19020 ) ;
#140704=EDGE_CURVE ( 'NONE', #40296, #68778, #39086, .T. ) ;
#140705=ORIENTED_EDGE ( 'NONE', *, *, #6457, .T. ) ;
#140706=EDGE_LOOP ( 'NONE', ( #51386, #121523, #7798, #95512 ) ) ;
#140707=EDGE_CURVE ( 'NONE', #41256, #103418, #117327, .T. ) ;
#140710=FACE_OUTER_BOUND ( 'NONE', #38367, .T. ) ;
#140711=EDGE_CURVE ( 'NONE', #69227, #111174, #23743, .T. ) ;
#140712=DIRECTION ( 'NONE',  ( 0.3543493200069162685, -0.000000000000000000, -0.9351131265310288487 ) ) ;
#140713=DIRECTION ( 'NONE',  ( -0.7071067811865487940, -0.7071067811865463515, -0.000000000000000000 ) ) ;
#140714=LINE ( 'NONE', #10200, #49231 ) ;
#140715=ADVANCED_FACE ( 'NONE', ( #49976 ), #127517, .F. ) ;
#140719=VERTEX_POINT ( 'NONE', #50670 ) ;
#140720=LINE ( 'NONE', #94365, #103544 ) ;
#140721=VERTEX_POINT ( 'NONE', #17322 ) ;
#140723=DIRECTION ( 'NONE',  ( 0.7071067811865487940, 0.7071067811865463515, 0.000000000000000000 ) ) ;
#140724=DIRECTION ( 'NONE',  ( 0.7071067811865487940, 0.7071067811865463515, 0.000000000000000000 ) ) ;
#140725=EDGE_LOOP ( 'NONE', ( #22350, #137619, #72938, #76855 ) ) ;
#140727=EDGE_CURVE ( 'NONE', #47662, #17057, #105732, .T. ) ;
#140728=VERTEX_POINT ( 'NONE', #138397 ) ;
#140729=DIRECTION ( 'NONE',  ( -0.7071067811865487940, 0.7071067811865463515, -0.000000000000000000 ) ) ;
#140730=EDGE_CURVE ( 'NONE', #14203, #138480, #115173, .T. ) ;
#140731=PLANE ( 'NONE',  #20677 ) ;
#140732=PLANE ( 'NONE',  #52431 ) ;
#140734=DIRECTION ( 'NONE',  ( -0.7071067811865487940, 0.7071067811865463515, -0.000000000000000000 ) ) ;
#140735=EDGE_CURVE ( 'NONE', #44234, #132762, #93467, .T. ) ;
#140737=EDGE_LOOP ( 'NONE', ( #109059, #12266, #103626, #40572 ) ) ;
#140738=FACE_OUTER_BOUND ( 'NONE', #102248, .T. ) ;
#140739=VERTEX_POINT ( 'NONE', #48534 ) ;
#140741=ADVANCED_FACE ( 'NONE', ( #92732 ), #139124, .F. ) ;
#140742=VERTEX_POINT ( 'NONE', #128247 ) ;
#140745=VERTEX_POINT ( 'NONE', #115893 ) ;
#140746=LINE ( 'NONE', #71249, #136341 ) ;
#140747=EDGE_CURVE ( 'NONE', #35520, #77121, #136973, .T. ) ;
#140748=CARTESIAN_POINT ( 'NONE',  ( 0.000000000000000000, -21.72500000000000142, 4.500000000000000888 ) ) ;
#140749=CARTESIAN_POINT ( 'NONE',  ( -34.36246187583878253, 22.22500000000000142, 4.000000000000000000 ) ) ;
#140750=FACE_BOUND ( 'NONE', #109470, .T. ) ;
#140752=DIRECTION ( 'NONE',  ( -0.7071067811865487940, 0.7071067811865463515, -0.000000000000000000 ) ) ;
#140753=CARTESIAN_POINT ( 'NONE',  ( -4.499999999999962697, -5.947814304570770538, 5.000000000000000000 ) ) ;
#140754=DIRECTION ( 'NONE',  ( -0.7071067811865486830, -0.7071067811865464625, 0.000000000000000000 ) ) ;
#140756=DIRECTION ( 'NONE',  ( -0.7071067811865486830, -0.7071067811865464625, 0.000000000000000000 ) ) ;
#140758=VERTEX_POINT ( 'NONE', #104310 ) ;
#140759=DIRECTION ( 'NONE',  ( -0.000000000000000000, 0.3543493200069153248, 0.9351131265310292928 ) ) ;
#140760=ORIENTED_EDGE ( 'NONE', *, *, #43363, .F. ) ;
#140764=VECTOR ( 'NONE', #40782, 1000.000000000000114 ) ;
#140765=DIRECTION ( 'NONE',  ( -0.7071067811865486830, 0.7071067811865464625, 0.000000000000000000 ) ) ;
#140767=ORIENTED_EDGE ( 'NONE', *, *, #136100, .T. ) ;
#140768=PLANE ( 'NONE',  #134872 ) ;
#140770=DIRECTION ( 'NONE',  ( 0.7071067811865487940, -0.7071067811865463515, 0.000000000000000000 ) ) ;
#140771=LINE ( 'NONE', #119720, #73629 ) ;
#140772=CARTESIAN_POINT ( 'NONE',  ( 13.49999999999991473, -1.592773361805351673, -6.492772025301255745 ) ) ;
#140773=CARTESIAN_POINT ( 'NONE',  ( 6.183988606268994381, 28.73617430169791476, 5.000000000000000000 ) ) ;
#140774=DIRECTION ( 'NONE',  ( -0.7071067811865486830, -0.7071067811865464625, 0.000000000000000000 ) ) ;
#140775=ORIENTED_EDGE ( 'NONE', *, *, #22081, .F. ) ;
#140776=EDGE_LOOP ( 'NONE', ( #54247, #55098, #7760, #101586 ) ) ;
#140777=DIRECTION ( 'NONE',  ( -0.3543493200069162685, -0.000000000000000000, -0.9351131265310288487 ) ) ;
#140778=VECTOR ( 'NONE', #142788, 1000.000000000000000 ) ;
#140779=PLANE ( 'NONE',  #49009 ) ;
#140780=ORIENTED_EDGE ( 'NONE', *, *, #6260, .F. ) ;
#140781=ORIENTED_EDGE ( 'NONE', *, *, #119618, .F. ) ;
#140783=ORIENTED_EDGE ( 'NONE', *, *, #133305, .T. ) ;
#140784=DIRECTION ( 'NONE',  ( 1.000000000000000000, 0.000000000000000000, 0.000000000000000000 ) ) ;
#140785=LINE ( 'NONE', #118273, #70706 ) ;
#140786=FACE_OUTER_BOUND ( 'NONE', #36900, .T. ) ;
#140787=VERTEX_POINT ( 'NONE', #16600 ) ;
#140788=DIRECTION ( 'NONE',  ( 0.3543493200069162685, -0.000000000000000000, -0.9351131265310288487 ) ) ;
#140789=VECTOR ( 'NONE', #12581, 1000.000000000000000 ) ;
#140790=AXIS2_PLACEMENT_3D ( 'NONE', #622, #22359, #98523 ) ;
#140791=( BOUNDED_CURVE ( )  B_SPLINE_CURVE ( 3, ( #79572, #44797, #11356, #91132 ),
 .UNSPECIFIED., .F., .T. ) 
 B_SPLINE_CURVE_WITH_KNOTS ( ( 4, 4 ),
 ( 4.350170835173026163, 4.500739107949268458 ),
 .UNSPECIFIED. ) 
 CURVE ( )  GEOMETRIC_REPRESENTATION_ITEM ( )  RATIONAL_B_SPLINE_CURVE ( ( 1.000000000000000000, 0.9981116584018941973, 0.9981116584018941973, 1.000000000000000000 ) ) 
 REPRESENTATION_ITEM ( '' )  );
#140792=CARTESIAN_POINT ( 'NONE',  ( 5.999999999999977796, -16.44781430457066662, 5.000000000000000000 ) ) ;
#140795=VERTEX_POINT ( 'NONE', #105047 ) ;
#140797=LINE ( 'NONE', #106016, #23433 ) ;
#140798=EDGE_CURVE ( 'NONE', #22078, #139771, #5710, .T. ) ;
#140799=DIRECTION ( 'NONE',  ( -0.000000000000000000, 0.000000000000000000, 1.000000000000000000 ) ) ;
#140801=ORIENTED_EDGE ( 'NONE', *, *, #24136, .T. ) ;
#140802=DIRECTION ( 'NONE',  ( 0.6830127018922180770, -0.6830127018922204085, -0.2588190451025213501 ) ) ;
#140803=VERTEX_POINT ( 'NONE', #33249 ) ;
#140804=FACE_OUTER_BOUND ( 'NONE', #6162, .T. ) ;
#140805=DIRECTION ( 'NONE',  ( 0.000000000000000000, 0.000000000000000000, 1.000000000000000000 ) ) ;
#140806=PLANE ( 'NONE',  #88893 ) ;
#140807=ORIENTED_EDGE ( 'NONE', *, *, #54619, .F. ) ;
#140808=ADVANCED_FACE ( 'NONE', ( #121618 ), #44092, .F. ) ;
#140809=LINE ( 'NONE', #23878, #47368 ) ;
#140811=CARTESIAN_POINT ( 'NONE',  ( 20.99999999999985079, -4.068876922607768343, 4.000000000000000000 ) ) ;
#140812=EDGE_LOOP ( 'NONE', ( #6932, #87555, #68142, #111484 ) ) ;
#140813=VECTOR ( 'NONE', #79771, 1000.000000000000227 ) ;
#140814=CARTESIAN_POINT ( 'NONE',  ( 26.20710678118635784, -5.240707523384230626, 5.000000000000000000 ) ) ;
#140815=LINE ( 'NONE', #53091, #28409 ) ;
#140816=AXIS2_PLACEMENT_3D ( 'NONE', #32268, #88073, #42455 ) ;
#140817=DIRECTION ( 'NONE',  ( 0.000000000000000000, 0.000000000000000000, -1.000000000000000000 ) ) ;
#140818=LINE ( 'NONE', #43670, #120217 ) ;
#140819=ADVANCED_FACE ( 'NONE', ( #110030 ), #76736, .F. ) ;
#140820=ORIENTED_EDGE ( 'NONE', *, *, #124514, .F. ) ;
#140822=ORIENTED_EDGE ( 'NONE', *, *, #100281, .F. ) ;
#140823=DIRECTION ( 'NONE',  ( -0.7071067811865486830, -0.7071067811865464625, -0.000000000000000000 ) ) ;
#140824=LINE ( 'NONE', #21204, #117709 ) ;
#140825=EDGE_CURVE ( 'NONE', #35675, #87648, #107180, .T. ) ;
#140828=CARTESIAN_POINT ( 'NONE',  ( -16.49999999999988276, -16.91253812416058722, 4.000000000000000000 ) ) ;
#140829=CARTESIAN_POINT ( 'NONE',  ( -45.48921356237309510, -27.52281430457087197, 5.000000000000000000 ) ) ;
#140830=ORIENTED_EDGE ( 'NONE', *, *, #95824, .F. ) ;
#140831=EDGE_CURVE ( 'NONE', #43903, #69745, #65873, .T. ) ;
#140832=DIRECTION ( 'NONE',  ( -0.7071067811865486830, 0.7071067811865464625, 0.000000000000000000 ) ) ;
#140834=VECTOR ( 'NONE', #110108, 1000.000000000000000 ) ;
#140837=FACE_OUTER_BOUND ( 'NONE', #109765, .T. ) ;
#140838=AXIS2_PLACEMENT_3D ( 'NONE', #97506, #100395, #108353 ) ;
#140839=EDGE_CURVE ( 'NONE', #91297, #83273, #7857, .T. ) ;
#140840=EDGE_LOOP ( 'NONE', ( #27033, #2333, #66590, #109286 ) ) ;
#140842=ORIENTED_EDGE ( 'NONE', *, *, #17501, .T. ) ;
#140843=VERTEX_POINT ( 'NONE', #54972 ) ;
#140844=DIRECTION ( 'NONE',  ( -0.000000000000000000, 0.000000000000000000, 1.000000000000000000 ) ) ;
#140845=CARTESIAN_POINT ( 'NONE',  ( 30.48921356237309510, -27.52281430457076894, 5.000000000000000000 ) ) ;
#140846=ADVANCED_FACE ( 'NONE', ( #120167 ), #20156, .F. ) ;
#140847=VERTEX_POINT ( 'NONE', #99139 ) ;
#140848=CARTESIAN_POINT ( 'NONE',  ( 18.08314806772920136, 21.75929247661550292, 7.311836541448091253 ) ) ;
#140849=LINE ( 'NONE', #75628, #139159 ) ;
#140850=CARTESIAN_POINT ( 'NONE',  ( 23.29289321881329755, 8.259292476615637923, 5.000000000000000000 ) ) ;
#140851=CARTESIAN_POINT ( 'NONE',  ( -24.97566027651206610, 3.896288752498341168, 4.156157854036512944 ) ) ;
#140855=CARTESIAN_POINT ( 'NONE',  ( 34.03163515922170035, 2.259292476615690770, 13.77329220150645384 ) ) ;
#140856=EDGE_CURVE ( 'NONE', #140742, #107457, #52096, .T. ) ;
#140857=CARTESIAN_POINT ( 'NONE',  ( 39.48921356237310221, -27.52281430457082934, 5.000000000000000000 ) ) ;
#140858=LINE ( 'NONE', #55315, #31631 ) ;
#140860=PLANE ( 'NONE',  #130118 ) ;
#140861=DIRECTION ( 'NONE',  ( 0.7071067811865487940, 0.7071067811865463515, -0.000000000000000000 ) ) ;
#140863=CARTESIAN_POINT ( 'NONE',  ( -26.99999999999980815, -6.033600742197676503, 5.000000000000000000 ) ) ;
#140864=ORIENTED_EDGE ( 'NONE', *, *, #98467, .F. ) ;
#140865=ORIENTED_EDGE ( 'NONE', *, *, #73686, .F. ) ;
#140867=DIRECTION ( 'NONE',  ( 0.7071067811865487940, -0.7071067811865463515, 0.000000000000000000 ) ) ;
#140870=FACE_OUTER_BOUND ( 'NONE', #10797, .T. ) ;
#140871=ORIENTED_EDGE ( 'NONE', *, *, #32491, .F. ) ;
#140872=FACE_OUTER_BOUND ( 'NONE', #124886, .T. ) ;
#140876=ORIENTED_EDGE ( 'NONE', *, *, #41255, .T. ) ;
#140877=DIRECTION ( 'NONE',  ( 0.7071067811865487940, -0.7071067811865463515, 0.000000000000000000 ) ) ;
#140878=ORIENTED_EDGE ( 'NONE', *, *, #93391, .F. ) ;
#140879=ORIENTED_EDGE ( 'NONE', *, *, #121765, .T. ) ;
#140881=VECTOR ( 'NONE', #23058, 1000.000000000000000 ) ;
#140883=VECTOR ( 'NONE', #53018, 1000.000000000000000 ) ;
#140884=EDGE_CURVE ( 'NONE', #33598, #103751, #53534, .T. ) ;
#140886=DIRECTION ( 'NONE',  ( 0.3543493200069162685, -0.000000000000000000, -0.9351131265310288487 ) ) ;
#140887=VECTOR ( 'NONE', #65383, 1000.000000000000227 ) ;
#140888=CARTESIAN_POINT ( 'NONE',  ( -2.292893218813436995, 20.25929247661551358, 5.000000000000000000 ) ) ;
#140890=EDGE_CURVE ( 'NONE', #66246, #92499, #109334, .T. ) ;
#140891=CARTESIAN_POINT ( 'NONE',  ( -5.700255128608413102, -27.71228299555201957, 4.000000000000000000 ) ) ;
#140892=AXIS2_PLACEMENT_3D ( 'NONE', #57076, #100560, #45489 ) ;
#140893=CARTESIAN_POINT ( 'NONE',  ( -31.49999999999977973, -12.08601207473292405, -10.46905243149087106 ) ) ;
#140894=ORIENTED_EDGE ( 'NONE', *, *, #6575, .T. ) ;
#140897=CARTESIAN_POINT ( 'NONE',  ( 20.99451991528748707, 28.92564299267952777, 4.000000000000000000 ) ) ;
#140898=CARTESIAN_POINT ( 'NONE',  ( -36.18398860626899705, 28.73617430169812437, 5.000000000000000000 ) ) ;
#140899=VECTOR ( 'NONE', #71824, 1000.000000000000000 ) ;
#140900=CARTESIAN_POINT ( 'NONE',  ( -32.99451991528749062, 28.92564299267960948, 4.000000000000000000 ) ) ;
#140901=CARTESIAN_POINT ( 'NONE',  ( 36.18398860626899705, 28.73617430169812437, 5.000000000000000000 ) ) ;
#140904=EDGE_CURVE ( 'NONE', #141462, #132753, #142680, .T. ) ;
#140905=FACE_OUTER_BOUND ( 'NONE', #93828, .T. ) ;
#140907=CARTESIAN_POINT ( 'NONE',  ( 15.48921356237309510, -27.52281430457066236, 5.000000000000000000 ) ) ;
#140908=CARTESIAN_POINT ( 'NONE',  ( -17.51078643762690845, -27.52281430457043143, 5.000000000000000000 ) ) ;
#140910=ORIENTED_EDGE ( 'NONE', *, *, #129911, .F. ) ;
#140911=ORIENTED_EDGE ( 'NONE', *, *, #141858, .T. ) ;
#140912=AXIS2_PLACEMENT_3D ( 'NONE', #127100, #16931, #43676 ) ;
#140913=PLANE ( 'NONE',  #56133 ) ;
#140915=EDGE_CURVE ( 'NONE', #51846, #72705, #47691, .T. ) ;
#140917=EDGE_LOOP ( 'NONE', ( #95964, #20365, #114911, #142020 ) ) ;
#140918=VECTOR ( 'NONE', #33057, 1000.000000000000227 ) ;
#140919=LINE ( 'NONE', #65561, #134744 ) ;
#140920=ORIENTED_EDGE ( 'NONE', *, *, #8361, .T. ) ;
#140921=LINE ( 'NONE', #138263, #53877 ) ;
#140922=CARTESIAN_POINT ( 'NONE',  ( -0.4892135623730947680, -27.52281430457055578, 5.000000000000000000 ) ) ;
#140923=VECTOR ( 'NONE', #126937, 1000.000000000000227 ) ;
#140924=AXIS2_PLACEMENT_3D ( 'NONE', #125588, #61764, #114672 ) ;
#140925=VECTOR ( 'NONE', #23330, 1000.000000000000000 ) ;
#140926=CARTESIAN_POINT ( 'NONE',  ( -11.67183060077638856, -18.74070752338409207, 4.000000000000000000 ) ) ;
#140927=CIRCLE ( 'NONE', #78450, 5.968999999999998529 ) ;
#140928=FACE_BOUND ( 'NONE', #23757, .T. ) ;
#140930=DIRECTION ( 'NONE',  ( 0.7071067811865486830, -0.7071067811865464625, -0.000000000000000000 ) ) ;
#140931=CARTESIAN_POINT ( 'NONE',  ( 17.81601139373099940, 28.73617430169775133, 5.000000000000000000 ) ) ;
#140932=CARTESIAN_POINT ( 'NONE',  ( 0.4892135623730947680, -27.52281430457055578, 5.000000000000000000 ) ) ;
#140933=ORIENTED_EDGE ( 'NONE', *, *, #64358, .T. ) ;
#140935=VECTOR ( 'NONE', #15598, 999.9999999999998863 ) ;
#140936=LINE ( 'NONE', #141677, #81153 ) ;
#140938=EDGE_LOOP ( 'NONE', ( #32015, #31402, #35174, #143505 ) ) ;
#140939=EDGE_CURVE ( 'NONE', #3772, #8318, #18660, .T. ) ;
#140940=ORIENTED_EDGE ( 'NONE', *, *, #49108, .F. ) ;
#140942=ORIENTED_EDGE ( 'NONE', *, *, #60602, .T. ) ;
#140943=CARTESIAN_POINT ( 'NONE',  ( 23.99999999999983302, -19.06887692260762179, 4.000000000000000000 ) ) ;
#140944=ORIENTED_EDGE ( 'NONE', *, *, #15382, .T. ) ;
#140945=DIRECTION ( 'NONE',  ( 0.7071067811865487940, 0.7071067811865463515, -0.000000000000000000 ) ) ;
#140946=VECTOR ( 'NONE', #85913, 999.9999999999998863 ) ;
#140947=CARTESIAN_POINT ( 'NONE',  ( -34.92500000000001137, 16.32446447596929318, 2.764066516344052094 ) ) ;
#140948=CARTESIAN_POINT ( 'NONE',  ( 1.828169399223519953, -5.240707523384232402, 4.000000000000000000 ) ) ;
#140949=CARTESIAN_POINT ( 'NONE',  ( -35.99451991528749772, 28.92564299267963079, 4.000000000000000000 ) ) ;
#140950=CARTESIAN_POINT ( 'NONE',  ( -33.18398860626899705, 28.73617430169810305, 5.000000000000000000 ) ) ;
#140952=DIRECTION ( 'NONE',  ( -0.6830127018922181881, 0.6830127018922202975, -0.2588190451025214056 ) ) ;
#140953=DIRECTION ( 'NONE',  ( 0.7071067811865486830, -0.7071067811865464625, -0.000000000000000000 ) ) ;
#140954=ORIENTED_EDGE ( 'NONE', *, *, #1413, .F. ) ;
#140955=ORIENTED_EDGE ( 'NONE', *, *, #37812, .T. ) ;
#140956=LINE ( 'NONE', #51125, #72758 ) ;
#140957=PLANE ( 'NONE',  #129916 ) ;
#140958=ORIENTED_EDGE ( 'NONE', *, *, #110163, .T. ) ;
#140959=ORIENTED_EDGE ( 'NONE', *, *, #78902, .T. ) ;
#140960=CARTESIAN_POINT ( 'NONE',  ( 57.29974487139158157, -27.71228299555246011, 4.000000000000000000 ) ) ;
#140961=EDGE_LOOP ( 'NONE', ( #86930, #75014, #124309, #51276 ) ) ;
#140963=VERTEX_POINT ( 'NONE', #11406 ) ;
#140967=ORIENTED_EDGE ( 'NONE', *, *, #59820, .T. ) ;
#140968=DIRECTION ( 'NONE',  ( 0.7071067811865487940, 0.7071067811865463515, 0.000000000000000000 ) ) ;
#140970=DIRECTION ( 'NONE',  ( 0.000000000000000000, 0.000000000000000000, 1.000000000000000000 ) ) ;
#140971=EDGE_CURVE ( 'NONE', #136929, #103105, #44076, .T. ) ;
#140972=CARTESIAN_POINT ( 'NONE',  ( 0.000000000000000000, -21.72500000000000142, 4.500000000000000888 ) ) ;
#140973=CARTESIAN_POINT ( 'NONE',  ( 31.49999999999977973, 6.277155672890302185, -3.510561720659014728 ) ) ;
#140974=ORIENTED_EDGE ( 'NONE', *, *, #95781, .F. ) ;
#140975=ORIENTED_EDGE ( 'NONE', *, *, #22081, .T. ) ;
#140977=PLANE ( 'NONE',  #26274 ) ;
#140978=ORIENTED_EDGE ( 'NONE', *, *, #75179, .F. ) ;
#140979=DIRECTION ( 'NONE',  ( -0.6830127018922181881, 0.6830127018922202975, -0.2588190451025214056 ) ) ;
#140980=ORIENTED_EDGE ( 'NONE', *, *, #5497, .F. ) ;
#140982=ORIENTED_EDGE ( 'NONE', *, *, #90905, .F. ) ;
#140983=LINE ( 'NONE', #76486, #65770 ) ;
#140984=VECTOR ( 'NONE', #105455, 1000.000000000000000 ) ;
#140985=VECTOR ( 'NONE', #133034, 1000.000000000000000 ) ;
#140986=VECTOR ( 'NONE', #23587, 1000.000000000000000 ) ;
#140987=LINE ( 'NONE', #75765, #9028 ) ;
#140988=DIRECTION ( 'NONE',  ( -0.7071067811865486830, -0.7071067811865464625, -0.000000000000000000 ) ) ;
#140990=EDGE_CURVE ( 'NONE', #105277, #110666, #1259, .T. ) ;
#140992=DIRECTION ( 'NONE',  ( -0.7071067811865487940, 0.7071067811865463515, -0.000000000000000000 ) ) ;
#140993=EDGE_CURVE ( 'NONE', #139777, #74065, #66554, .T. ) ;
#140994=ADVANCED_FACE ( 'NONE', ( #23000 ), #99885, .F. ) ;
#140995=ORIENTED_EDGE ( 'NONE', *, *, #59686, .T. ) ;
#140997=ORIENTED_EDGE ( 'NONE', *, *, #42424, .F. ) ;
#140999=LINE ( 'NONE', #41706, #51756 ) ;
#141000=ADVANCED_FACE ( 'NONE', ( #2695 ), #78149, .F. ) ;
#141003=VERTEX_POINT ( 'NONE', #36758 ) ;
#141004=DIRECTION ( 'NONE',  ( 0.7071067811865487940, -0.7071067811865463515, 0.000000000000000000 ) ) ;
#141005=LINE ( 'NONE', #41711, #90711 ) ;
#141006=VERTEX_POINT ( 'NONE', #552 ) ;
#141008=EDGE_CURVE ( 'NONE', #20953, #130029, #91182, .T. ) ;
#141009=LINE ( 'NONE', #54058, #51130 ) ;
#141010=LINE ( 'NONE', #75089, #65068 ) ;
#141011=DIRECTION ( 'NONE',  ( 1.000000000000000000, 0.000000000000000000, 0.000000000000000000 ) ) ;
#141013=FACE_OUTER_BOUND ( 'NONE', #45169, .T. ) ;
#141016=( BOUNDED_CURVE ( )  B_SPLINE_CURVE ( 3, ( #106764, #51709, #129970, #85730 ),
 .UNSPECIFIED., .F., .F. ) 
 B_SPLINE_CURVE_WITH_KNOTS ( ( 4, 4 ),
 ( 1.901594255663618060, 1.933014472006549633 ),
 .UNSPECIFIED. ) 
 CURVE ( )  GEOMETRIC_REPRESENTATION_ITEM ( )  RATIONAL_B_SPLINE_CURVE ( ( 1.000000000000000000, 0.9999177325257868620, 0.9999177325257868620, 1.000000000000000000 ) ) 
 REPRESENTATION_ITEM ( '' )  );
#141017=LINE ( 'NONE', #142476, #99624 ) ;
#141018=ADVANCED_FACE ( 'NONE', ( #12152 ), #33931, .F. ) ;
#141019=VECTOR ( 'NONE', #53144, 999.9999999999998863 ) ;
#141020=CARTESIAN_POINT ( 'NONE',  ( 20.99451991528748707, 28.92564299267952777, 4.000000000000000000 ) ) ;
#141021=CARTESIAN_POINT ( 'NONE',  ( -18.18398860626898994, 28.73617430169800002, 5.000000000000000000 ) ) ;
#141022=LINE ( 'NONE', #85211, #37417 ) ;
#141023=VERTEX_POINT ( 'NONE', #135399 ) ;
#141024=CARTESIAN_POINT ( 'NONE',  ( -34.82816939922327748, 3.759292476615692102, 4.000000000000000000 ) ) ;
#141025=ORIENTED_EDGE ( 'NONE', *, *, #7723, .T. ) ;
#141026=LINE ( 'NONE', #130182, #24658 ) ;
#141028=EDGE_LOOP ( 'NONE', ( #50512, #74819, #14779, #94973 ) ) ;
#141029=VECTOR ( 'NONE', #101096, 1000.000000000000000 ) ;
#141031=DIRECTION ( 'NONE',  ( 0.7071067811865486830, -0.7071067811865464625, -0.000000000000000000 ) ) ;
#141032=CARTESIAN_POINT ( 'NONE',  ( -24.32816939922335919, -3.740707523384244837, 4.000000000000000000 ) ) ;
#141034=DIRECTION ( 'NONE',  ( 0.7071067811865487940, 0.7071067811865463515, 0.000000000000000000 ) ) ;
#141035=PLANE ( 'NONE',  #78793 ) ;
#141038=ORIENTED_EDGE ( 'NONE', *, *, #54819, .T. ) ;
#141040=LINE ( 'NONE', #85960, #58374 ) ;
#141042=EDGE_CURVE ( 'NONE', #109446, #114222, #122323, .T. ) ;
#141043=VECTOR ( 'NONE', #98034, 1000.000000000000000 ) ;
#141044=DIRECTION ( 'NONE',  ( 0.3543493200069162685, -0.000000000000000000, -0.9351131265310288487 ) ) ;
#141046=CARTESIAN_POINT ( 'NONE',  ( -13.49999999999989697, -17.56887692260763245, 4.000000000000000000 ) ) ;
#141047=DIRECTION ( 'NONE',  ( 1.000000000000000000, -0.000000000000000000, 0.000000000000000000 ) ) ;
#141048=ORIENTED_EDGE ( 'NONE', *, *, #109193, .F. ) ;
#141049=DIRECTION ( 'NONE',  ( -0.7071067811865486830, 0.7071067811865464625, 0.000000000000000000 ) ) ;
#141050=DIRECTION ( 'NONE',  ( 0.6830127018922180770, -0.6830127018922204085, -0.2588190451025213501 ) ) ;
#141053=VECTOR ( 'NONE', #101608, 1000.000000000000000 ) ;
#141054=VERTEX_POINT ( 'NONE', #80302 ) ;
#141055=PLANE ( 'NONE',  #95351 ) ;
#141056=EDGE_CURVE ( 'NONE', #4889, #58332, #124491, .T. ) ;
#141057=ORIENTED_EDGE ( 'NONE', *, *, #99069, .T. ) ;
#141060=LINE ( 'NONE', #139682, #117150 ) ;
#141061=CARTESIAN_POINT ( 'NONE',  ( 24.99033360189226016, 3.759292476615681888, 4.478963035907999490 ) ) ;
#141062=ORIENTED_EDGE ( 'NONE', *, *, #66746, .F. ) ;
#141063=CARTESIAN_POINT ( 'NONE',  ( 4.499999999999972466, 3.431123077392145948, 4.000000000000000000 ) ) ;
#141064=EDGE_CURVE ( 'NONE', #128234, #78195, #133945, .T. ) ;
#141066=LINE ( 'NONE', #109161, #101809 ) ;
#141068=CARTESIAN_POINT ( 'NONE',  ( 45.29974487139158867, -27.71228299555237840, 4.000000000000000000 ) ) ;
#141069=ORIENTED_EDGE ( 'NONE', *, *, #54736, .T. ) ;
#141070=CARTESIAN_POINT ( 'NONE',  ( -29.99451991528749417, 28.92564299267958816, 4.000000000000000000 ) ) ;
#141072=ADVANCED_FACE ( 'NONE', ( #34637 ), #123081, .F. ) ;
#141073=DIRECTION ( 'NONE',  ( 0.6830127018922180770, -0.6830127018922204085, -0.2588190451025213501 ) ) ;
#141074=VERTEX_POINT ( 'NONE', #136793 ) ;
#141075=ORIENTED_EDGE ( 'NONE', *, *, #47305, .F. ) ;
#141078=ADVANCED_FACE ( 'NONE', ( #25895 ), #6946, .F. ) ;
#141079=CARTESIAN_POINT ( 'NONE',  ( 0.4892135623730947680, -27.52281430457055578, 5.000000000000000000 ) ) ;
#141081=DIRECTION ( 'NONE',  ( -0.000000000000000000, 0.3543493200069153248, 0.9351131265310292928 ) ) ;
#141082=ORIENTED_EDGE ( 'NONE', *, *, #27628, .F. ) ;
#141083=CARTESIAN_POINT ( 'NONE',  ( -6.888376381052371933, 9.759292476615621936, 17.35367589129214494 ) ) ;
#141084=PLANE ( 'NONE',  #44377 ) ;
#141085=VERTEX_POINT ( 'NONE', #95426 ) ;
#141087=FACE_OUTER_BOUND ( 'NONE', #119391, .T. ) ;
#141088=DIRECTION ( 'NONE',  ( -0.6830127018922181881, 0.6830127018922202975, -0.2588190451025214056 ) ) ;
#141089=CIRCLE ( 'NONE', #78610, 5.968999999999998529 ) ;
#141091=VECTOR ( 'NONE', #65439, 1000.000000000000000 ) ;
#141092=VERTEX_POINT ( 'NONE', #4796 ) ;
#141093=ORIENTED_EDGE ( 'NONE', *, *, #119759, .T. ) ;
#141094=VECTOR ( 'NONE', #46137, 1000.000000000000000 ) ;
#141095=FACE_BOUND ( 'NONE', #96898, .T. ) ;
#141096=DIRECTION ( 'NONE',  ( 0.6830127018922181881, 0.6830127018922202975, -0.2588190451025214056 ) ) ;
#141097=LINE ( 'NONE', #109194, #99910 ) ;
#141098=CARTESIAN_POINT ( 'NONE',  ( -24.18398860626899705, 28.73617430169804265, 5.000000000000000000 ) ) ;
#141100=CARTESIAN_POINT ( 'NONE',  ( -39.18398860626899705, 28.73617430169814568, 5.000000000000000000 ) ) ;
#141101=DIRECTION ( 'NONE',  ( -0.000000000000000000, 0.3543493200069153248, 0.9351131265310292928 ) ) ;
#141104=VECTOR ( 'NONE', #58342, 999.9999999999998863 ) ;
#141105=ORIENTED_EDGE ( 'NONE', *, *, #8996, .T. ) ;
#141106=ORIENTED_EDGE ( 'NONE', *, *, #35562, .T. ) ;
#141107=ORIENTED_EDGE ( 'NONE', *, *, #106042, .F. ) ;
#141109=VECTOR ( 'NONE', #55931, 1000.000000000000000 ) ;
#141111=EDGE_CURVE ( 'NONE', #47430, #80191, #138227, .T. ) ;
#141113=VECTOR ( 'NONE', #112901, 1000.000000000000000 ) ;
#141114=FACE_OUTER_BOUND ( 'NONE', #41540, .T. ) ;
#141115=EDGE_CURVE ( 'NONE', #78905, #44742, #28765, .T. ) ;
#141116=ORIENTED_EDGE ( 'NONE', *, *, #138269, .F. ) ;
#141117=LINE ( 'NONE', #84621, #143181 ) ;
#141118=LINE ( 'NONE', #31668, #132841 ) ;
#141119=PLANE ( 'NONE',  #138398 ) ;
#141120=LINE ( 'NONE', #140419, #67027 ) ;
#141121=VECTOR ( 'NONE', #71959, 1000.000000000000000 ) ;
#141122=CARTESIAN_POINT ( 'NONE',  ( -12.79289321881336328, -14.24070752338414358, 5.000000000000000000 ) ) ;
#141123=ORIENTED_EDGE ( 'NONE', *, *, #90476, .T. ) ;
#141124=AXIS2_PLACEMENT_3D ( 'NONE', #33571, #121948, #55305 ) ;
#141125=CARTESIAN_POINT ( 'NONE',  ( 66.18398860626901126, 28.73617430169833753, 5.000000000000000000 ) ) ;
#141127=VECTOR ( 'NONE', #121762, 1000.000000000000000 ) ;
#141129=CARTESIAN_POINT ( 'NONE',  ( -69.48921356237309510, -27.52281430457103895, 5.000000000000000000 ) ) ;
#141130=ORIENTED_EDGE ( 'NONE', *, *, #123139, .T. ) ;
#141132=ORIENTED_EDGE ( 'NONE', *, *, #66429, .T. ) ;
#141136=VECTOR ( 'NONE', #69975, 1000.000000000000000 ) ;
#141137=ORIENTED_EDGE ( 'NONE', *, *, #129155, .F. ) ;
#141138=ORIENTED_EDGE ( 'NONE', *, *, #103001, .F. ) ;
#141139=CARTESIAN_POINT ( 'NONE',  ( 7.499999999999951150, -10.91253812416064584, 4.000000000000000000 ) ) ;
#141142=LINE ( 'NONE', #109237, #107330 ) ;
#141143=DIRECTION ( 'NONE',  ( 0.7071067811865486830, -0.7071067811865464625, -0.000000000000000000 ) ) ;
#141144=EDGE_LOOP ( 'NONE', ( #125349, #40791, #61935, #56126 ) ) ;
#141145=DIRECTION ( 'NONE',  ( 0.7071067811865487940, 0.7071067811865463515, 0.000000000000000000 ) ) ;
#141146=AXIS2_PLACEMENT_3D ( 'NONE', #134466, #35170, #56228 ) ;
#141148=PLANE ( 'NONE',  #120793 ) ;
#141149=CARTESIAN_POINT ( 'NONE',  ( -8.510786437626906675, -27.52281430457049183, 5.000000000000000000 ) ) ;
#141151=CARTESIAN_POINT ( 'NONE',  ( 34.49999999999975842, 1.464255608400477415, 4.994342998332161443 ) ) ;
#141153=ORIENTED_EDGE ( 'NONE', *, *, #28641, .F. ) ;
#141155=ORIENTED_EDGE ( 'NONE', *, *, #22856, .T. ) ;
#141157=ORIENTED_EDGE ( 'NONE', *, *, #101167, .F. ) ;
#141158=EDGE_CURVE ( 'NONE', #80458, #110318, #38212, .T. ) ;
#141161=PLANE ( 'NONE',  #50975 ) ;
#141163=EDGE_LOOP ( 'NONE', ( #22551, #20999, #73612, #31868 ) ) ;
#141165=ORIENTED_EDGE ( 'NONE', *, *, #95006, .T. ) ;
#141166=EDGE_CURVE ( 'NONE', #119486, #125242, #139690, .T. ) ;
#141167=ADVANCED_FACE ( 'NONE', ( #94694 ), #49099, .F. ) ;
#141170=EDGE_CURVE ( 'NONE', #84015, #95610, #27300, .T. ) ;
#141171=FACE_OUTER_BOUND ( 'NONE', #75187, .T. ) ;
#141173=ORIENTED_EDGE ( 'NONE', *, *, #101928, .F. ) ;
#141174=VERTEX_POINT ( 'NONE', #17839 ) ;
#141175=ADVANCED_FACE ( 'NONE', ( #105569 ), #39656, .F. ) ;
#141176=ORIENTED_EDGE ( 'NONE', *, *, #18592, .T. ) ;
#141177=CARTESIAN_POINT ( 'NONE',  ( 26.99999999999980105, -13.39766691384881092, -10.96608748226472052 ) ) ;
#141178=DIRECTION ( 'NONE',  ( -0.7071067811865486830, -0.7071067811865464625, 0.000000000000000000 ) ) ;
#141179=EDGE_CURVE ( 'NONE', #50236, #139610, #6231, .T. ) ;
#141180=CARTESIAN_POINT ( 'NONE',  ( -14.47599861414540356, 22.03583458319439004, 4.979811245910085837 ) ) ;
#141181=DIRECTION ( 'NONE',  ( 0.7071067811865487940, 0.7071067811865463515, -0.000000000000000000 ) ) ;
#141183=VECTOR ( 'NONE', #3493, 1000.000000000000000 ) ;
#141184=CARTESIAN_POINT ( 'NONE',  ( 9.489213562373095101, -27.52281430457062328, 5.000000000000000000 ) ) ;
#141186=DIRECTION ( 'NONE',  ( 0.7071067811865487940, 0.7071067811865463515, 0.000000000000000000 ) ) ;
#141187=ORIENTED_EDGE ( 'NONE', *, *, #41118, .T. ) ;
#141188=PLANE ( 'NONE',  #64874 ) ;
#141190=VECTOR ( 'NONE', #46194, 1000.000000000000000 ) ;
#141192=LINE ( 'NONE', #44805, #24512 ) ;
#141193=ORIENTED_EDGE ( 'NONE', *, *, #80106, .T. ) ;
#141195=EDGE_CURVE ( 'NONE', #114640, #7978, #5546, .T. ) ;
#141197=ORIENTED_EDGE ( 'NONE', *, *, #134682, .T. ) ;
#141198=CARTESIAN_POINT ( 'NONE',  ( 57.18398860626899705, 28.73617430169827358, 5.000000000000000000 ) ) ;
#141199=ORIENTED_EDGE ( 'NONE', *, *, #35749, .T. ) ;
#141200=DIRECTION ( 'NONE',  ( -0.7071067811865486830, -0.7071067811865464625, 0.000000000000000000 ) ) ;
#141201=VERTEX_POINT ( 'NONE', #50508 ) ;
#141202=PLANE ( 'NONE',  #95249 ) ;
#141203=VECTOR ( 'NONE', #47508, 1000.000000000000227 ) ;
#141204=EDGE_LOOP ( 'NONE', ( #140491, #81286, #104751 ) ) ;
#141205=( BOUNDED_CURVE ( )  B_SPLINE_CURVE ( 3, ( #40500, #7828, #8511, #20130 ),
 .UNSPECIFIED., .F., .T. ) 
 B_SPLINE_CURVE_WITH_KNOTS ( ( 4, 4 ),
 ( 2.280733380739273120, 2.329266631601943693 ),
 .UNSPECIFIED. ) 
 CURVE ( )  GEOMETRIC_REPRESENTATION_ITEM ( )  RATIONAL_B_SPLINE_CURVE ( ( 1.000000000000000000, 0.9998037199289477872, 0.9998037199289477872, 1.000000000000000000 ) ) 
 REPRESENTATION_ITEM ( '' )  );
#141206=EDGE_CURVE ( 'NONE', #126973, #95699, #128086, .T. ) ;
#141207=FACE_OUTER_BOUND ( 'NONE', #126233, .T. ) ;
#141209=DIRECTION ( 'NONE',  ( 0.7071067811865487940, -0.7071067811865463515, 0.000000000000000000 ) ) ;
#141210=DIRECTION ( 'NONE',  ( -0.000000000000000000, -0.3543493200069152138, 0.9351131265310292928 ) ) ;
#141211=DIRECTION ( 'NONE',  ( -0.7071067811865486830, 0.7071067811865464625, 0.000000000000000000 ) ) ;
#141212=LINE ( 'NONE', #71706, #3148 ) ;
#141213=DIRECTION ( 'NONE',  ( 0.7071067811865487940, 0.7071067811865463515, -0.000000000000000000 ) ) ;
#141216=VECTOR ( 'NONE', #138570, 1000.000000000000000 ) ;
#141217=VECTOR ( 'NONE', #78143, 999.9999999999998863 ) ;
#141218=FACE_OUTER_BOUND ( 'NONE', #19201, .T. ) ;
#141219=CARTESIAN_POINT ( 'NONE',  ( -42.48921356237308800, -27.52281430457085065, 5.000000000000000000 ) ) ;
#141221=EDGE_LOOP ( 'NONE', ( #76968, #74106, #111810, #81349 ) ) ;
#141222=VECTOR ( 'NONE', #16233, 1000.000000000000000 ) ;
#141223=DIRECTION ( 'NONE',  ( -0.7071067811865486830, -0.7071067811865464625, -0.000000000000000000 ) ) ;
#141224=VERTEX_POINT ( 'NONE', #83881 ) ;
#141225=EDGE_CURVE ( 'NONE', #115259, #138298, #73013, .T. ) ;
#141229=PLANE ( 'NONE',  #25527 ) ;
#141231=ORIENTED_EDGE ( 'NONE', *, *, #133427, .F. ) ;
#141233=CARTESIAN_POINT ( 'NONE',  ( -2.510786437626908008, -27.52281430457053446, 5.000000000000000000 ) ) ;
#141234=EDGE_CURVE ( 'NONE', #6614, #110607, #85985, .T. ) ;
#141236=VECTOR ( 'NONE', #80554, 1000.000000000000227 ) ;
#141238=DIRECTION ( 'NONE',  ( -0.000000000000000000, -0.000000000000000000, 1.000000000000000000 ) ) ;
#141240=LINE ( 'NONE', #53538, #11895 ) ;
#141241=VECTOR ( 'NONE', #140036, 1000.000000000000000 ) ;
#141243=CARTESIAN_POINT ( 'NONE',  ( -21.79289321881330110, -20.24070752338407075, 5.000000000000000000 ) ) ;
#141244=EDGE_CURVE ( 'NONE', #140847, #78830, #128772, .T. ) ;
#141246=VERTEX_POINT ( 'NONE', #19993 ) ;
#141250=VECTOR ( 'NONE', #59675, 999.9999999999998863 ) ;
#141251=ORIENTED_EDGE ( 'NONE', *, *, #41405, .F. ) ;
#141252=EDGE_CURVE ( 'NONE', #52888, #108664, #130942, .T. ) ;
#141254=VECTOR ( 'NONE', #118945, 1000.000000000000000 ) ;
#141256=ORIENTED_EDGE ( 'NONE', *, *, #60189, .F. ) ;
#141258=CARTESIAN_POINT ( 'NONE',  ( -8.187538124160473885, -22.22500000000000142, 4.000000000000000000 ) ) ;
#141261=ADVANCED_FACE ( 'NONE', ( #140361 ), #41053, .F. ) ;
#141262=CARTESIAN_POINT ( 'NONE',  ( 11.99451991528749417, 28.92564299267946382, 4.000000000000000000 ) ) ;
#141263=DIRECTION ( 'NONE',  ( -0.7071067811865486830, -0.7071067811865464625, 0.000000000000000000 ) ) ;
#141265=VECTOR ( 'NONE', #122063, 1000.000000000000000 ) ;
#141266=CARTESIAN_POINT ( 'NONE',  ( 7.499999999999954703, 6.277155672890280869, -3.510561720658957441 ) ) ;
#141267=ORIENTED_EDGE ( 'NONE', *, *, #8647, .T. ) ;
#141268=ORIENTED_EDGE ( 'NONE', *, *, #123938, .T. ) ;
#141269=EDGE_CURVE ( 'NONE', #5220, #48400, #109875, .T. ) ;
#141270=ORIENTED_EDGE ( 'NONE', *, *, #131889, .T. ) ;
#141271=CARTESIAN_POINT ( 'NONE',  ( 10.49999999999993605, -5.947814304570766986, 5.000000000000000000 ) ) ;
#141272=EDGE_CURVE ( 'NONE', #139596, #115334, #96127, .T. ) ;
#141273=CARTESIAN_POINT ( 'NONE',  ( -18.18398860626898994, 28.73617430169800002, 5.000000000000000000 ) ) ;
#141275=VECTOR ( 'NONE', #88829, 1000.000000000000000 ) ;
#141276=DIRECTION ( 'NONE',  ( -0.6830127018922180770, -0.6830127018922204085, -0.2588190451025213501 ) ) ;
#141278=EDGE_CURVE ( 'NONE', #13019, #93595, #10539, .T. ) ;
#141279=ORIENTED_EDGE ( 'NONE', *, *, #51057, .T. ) ;
#141282=ORIENTED_EDGE ( 'NONE', *, *, #66607, .T. ) ;
#141283=EDGE_LOOP ( 'NONE', ( #83195, #14468, #115072, #76507 ) ) ;
#141284=AXIS2_PLACEMENT_3D ( 'NONE', #49050, #124445, #25846 ) ;
#141285=ADVANCED_FACE ( 'NONE', ( #29447 ), #54802, .F. ) ;
#141290=EDGE_CURVE ( 'NONE', #134483, #93602, #86717, .T. ) ;
#141291=ORIENTED_EDGE ( 'NONE', *, *, #51792, .T. ) ;
#141292=DIRECTION ( 'NONE',  ( -0.7071067811865487940, 0.7071067811865463515, -0.000000000000000000 ) ) ;
#141294=VECTOR ( 'NONE', #116854, 999.9999999999998863 ) ;
#141296=PLANE ( 'NONE',  #34529 ) ;
#141298=AXIS2_PLACEMENT_3D ( 'NONE', #58890, #126912, #114616 ) ;
#141299=VECTOR ( 'NONE', #141178, 1000.000000000000000 ) ;
#141301=LINE ( 'NONE', #42014, #116072 ) ;
#141302=VERTEX_POINT ( 'NONE', #9085 ) ;
#141303=AXIS2_PLACEMENT_3D ( 'NONE', #67934, #54195, #88220 ) ;
#141305=ORIENTED_EDGE ( 'NONE', *, *, #25145, .F. ) ;
#141307=DIRECTION ( 'NONE',  ( -0.6830127018922180770, -0.6830127018922204085, -0.2588190451025213501 ) ) ;
#141308=EDGE_LOOP ( 'NONE', ( #22309, #53260, #43964, #18092 ) ) ;
#141309=EDGE_CURVE ( 'NONE', #97669, #22290, #120743, .T. ) ;
#141310=ORIENTED_EDGE ( 'NONE', *, *, #3667, .T. ) ;
#141311=PLANE ( 'NONE',  #113071 ) ;
#141312=ORIENTED_EDGE ( 'NONE', *, *, #120521, .T. ) ;
#141313=ORIENTED_EDGE ( 'NONE', *, *, #63054, .F. ) ;
#141315=VERTEX_POINT ( 'NONE', #21449 ) ;
#141317=PLANE ( 'NONE',  #83111 ) ;
#141320=CARTESIAN_POINT ( 'NONE',  ( -7.499999999999958256, 19.08746187583906462, 4.000000000000000000 ) ) ;
#141321=CARTESIAN_POINT ( 'NONE',  ( -18.48921356237309510, -27.52281430457068367, 5.000000000000000000 ) ) ;
#141322=DIRECTION ( 'NONE',  ( 0.7071067811865486830, -0.7071067811865464625, -0.000000000000000000 ) ) ;
#141323=DIRECTION ( 'NONE',  ( -0.000000000000000000, -0.3543493200069152693, 0.9351131265310292928 ) ) ;
#141324=VECTOR ( 'NONE', #96976, 1000.000000000000227 ) ;
#141325=CARTESIAN_POINT ( 'NONE',  ( 4.734933297179464873, 12.75929247661558286, 18.34774599283955254 ) ) ;
#141326=AXIS2_PLACEMENT_3D ( 'NONE', #23047, #135437, #57888 ) ;
#141327=DIRECTION ( 'NONE',  ( 0.7071067811865486830, -0.7071067811865464625, -0.000000000000000000 ) ) ;
#141328=VECTOR ( 'NONE', #79860, 1000.000000000000000 ) ;
#141329=CARTESIAN_POINT ( 'NONE',  ( -5.999999999999952927, -7.447814304570758104, 5.000000000000000000 ) ) ;
#141330=LINE ( 'NONE', #51488, #116556 ) ;
#141331=ORIENTED_EDGE ( 'NONE', *, *, #124396, .F. ) ;
#141332=VECTOR ( 'NONE', #75633, 1000.000000000000227 ) ;
#141334=ORIENTED_EDGE ( 'NONE', *, *, #7060, .F. ) ;
#141335=EDGE_LOOP ( 'NONE', ( #113574, #33177, #139050, #77844 ) ) ;
#141337=ORIENTED_EDGE ( 'NONE', *, *, #95993, .F. ) ;
#141338=AXIS2_PLACEMENT_3D ( 'NONE', #87195, #41527, #51008 ) ;
#141339=EDGE_LOOP ( 'NONE', ( #7780, #18157, #49327, #114235 ) ) ;
#141340=CARTESIAN_POINT ( 'NONE',  ( 0.000000000000000000, 0.000000000000000000, 5.000000000000000000 ) ) ;
#141341=CARTESIAN_POINT ( 'NONE',  ( -34.92500000000001137, -22.22500000000000142, 4.500000000000000888 ) ) ;
#141343=CARTESIAN_POINT ( 'NONE',  ( 7.828169399223476432, -14.24070752338413293, 4.000000000000000000 ) ) ;
#141345=DIRECTION ( 'NONE',  ( -0.000000000000000000, -0.3543493200069152693, 0.9351131265310292928 ) ) ;
#141346=ORIENTED_EDGE ( 'NONE', *, *, #7603, .F. ) ;
#141347=LINE ( 'NONE', #128357, #7928 ) ;
#141348=ADVANCED_FACE ( 'NONE', ( #117857 ), #142526, .F. ) ;
#141351=VERTEX_POINT ( 'NONE', #63557 ) ;
#141353=EDGE_CURVE ( 'NONE', #94963, #108745, #129476, .T. ) ;
#141354=DIRECTION ( 'NONE',  ( -0.000000000000000000, 0.3543493200069153248, 0.9351131265310292928 ) ) ;
#141355=ADVANCED_FACE ( 'NONE', ( #107011 ), #120001, .T. ) ;
#141359=ORIENTED_EDGE ( 'NONE', *, *, #45064, .T. ) ;
#141360=ADVANCED_FACE ( 'NONE', ( #84574 ), #141815, .F. ) ;
#141361=DIRECTION ( 'NONE',  ( -0.7071067811865486830, -0.7071067811865464625, 0.000000000000000000 ) ) ;
#141362=AXIS2_PLACEMENT_3D ( 'NONE', #65142, #141987, #65872 ) ;
#141363=VERTEX_POINT ( 'NONE', #64971 ) ;
#141364=CARTESIAN_POINT ( 'NONE',  ( 9.005480084712511157, 28.92564299267931816, 4.000000000000000000 ) ) ;
#141365=LINE ( 'NONE', #140640, #65041 ) ;
#141366=DIRECTION ( 'NONE',  ( 0.000000000000000000, 0.000000000000000000, -1.000000000000000000 ) ) ;
#141367=EDGE_CURVE ( 'NONE', #90068, #61512, #109160, .T. ) ;
#141368=LINE ( 'NONE', #76121, #105100 ) ;
#141369=VERTEX_POINT ( 'NONE', #65712 ) ;
#141370=CARTESIAN_POINT ( 'NONE',  ( 6.792893218813411238, -20.24070752338407431, 5.000000000000000000 ) ) ;
#141371=EDGE_CURVE ( 'NONE', #37438, #72185, #91006, .T. ) ;
#141372=DIRECTION ( 'NONE',  ( 0.7071067811865487940, 0.7071067811865463515, 0.000000000000000000 ) ) ;
#141373=CARTESIAN_POINT ( 'NONE',  ( -33.18398860626899705, 28.73617430169810305, 5.000000000000000000 ) ) ;
#141374=ORIENTED_EDGE ( 'NONE', *, *, #25016, .F. ) ;
#141376=VECTOR ( 'NONE', #141345, 1000.000000000000000 ) ;
#141377=CARTESIAN_POINT ( 'NONE',  ( -32.20710678118631876, 18.75929247661553489, 5.000000000000000000 ) ) ;
#141378=VERTEX_POINT ( 'NONE', #55515 ) ;
#141379=EDGE_CURVE ( 'NONE', #138104, #104458, #101853, .T. ) ;
#141382=ORIENTED_EDGE ( 'NONE', *, *, #70576, .F. ) ;
#141383=ADVANCED_FACE ( 'NONE', ( #35202 ), #12686, .F. ) ;
#141384=CARTESIAN_POINT ( 'NONE',  ( 27.29974487139158512, -27.71228299555225405, 4.000000000000000000 ) ) ;
#141385=DIRECTION ( 'NONE',  ( -0.000000000000000000, 0.000000000000000000, 1.000000000000000000 ) ) ;
#141386=AXIS2_PLACEMENT_3D ( 'NONE', #14648, #92184, #92916 ) ;
#141387=ORIENTED_EDGE ( 'NONE', *, *, #15035, .T. ) ;
#141388=DIRECTION ( 'NONE',  ( -0.000000000000000000, 0.3543493200069153248, 0.9351131265310292928 ) ) ;
#141389=EDGE_CURVE ( 'NONE', #115605, #125405, #133092, .T. ) ;
#141390=CARTESIAN_POINT ( 'NONE',  ( 0.2997448713915885632, -27.71228299555206220, 4.000000000000000000 ) ) ;
#141391=DIRECTION ( 'NONE',  ( -0.7071067811865486830, -0.7071067811865464625, 0.000000000000000000 ) ) ;
#141394=CARTESIAN_POINT ( 'NONE',  ( 45.48921356237309510, -27.52281430457087197, 5.000000000000000000 ) ) ;
#141395=DIRECTION ( 'NONE',  ( -0.6830127018922181881, 0.6830127018922202975, -0.2588190451025214056 ) ) ;
#141396=EDGE_CURVE ( 'NONE', #110142, #121003, #35918, .T. ) ;
#141397=LINE ( 'NONE', #42113, #8716 ) ;
#141398=CARTESIAN_POINT ( 'NONE',  ( 25.49999999999982947, -1.912538124160735542, 4.000000000000000000 ) ) ;
#141399=DIRECTION ( 'NONE',  ( -0.7071067811865486830, -0.7071067811865464625, 0.000000000000000000 ) ) ;
#141400=VECTOR ( 'NONE', #39608, 1000.000000000000000 ) ;
#141401=DIRECTION ( 'NONE',  ( 1.000000000000000000, 0.000000000000000000, 0.000000000000000000 ) ) ;
#141402=FACE_OUTER_BOUND ( 'NONE', #37025, .T. ) ;
#141404=ORIENTED_EDGE ( 'NONE', *, *, #51338, .F. ) ;
#141405=VERTEX_POINT ( 'NONE', #14117 ) ;
#141406=VECTOR ( 'NONE', #115226, 999.9999999999998863 ) ;
#141410=EDGE_LOOP ( 'NONE', ( #82394, #81062, #130356, #120491 ) ) ;
#141411=VERTEX_POINT ( 'NONE', #22134 ) ;
#141412=ADVANCED_FACE ( 'NONE', ( #124319 ), #56263, .F. ) ;
#141413=LINE ( 'NONE', #85588, #124313 ) ;
#141415=VECTOR ( 'NONE', #98738, 999.9999999999998863 ) ;
#141416=VECTOR ( 'NONE', #128895, 1000.000000000000227 ) ;
#141417=VECTOR ( 'NONE', #81327, 1000.000000000000000 ) ;
#141421=AXIS2_PLACEMENT_3D ( 'NONE', #46165, #14204, #102671 ) ;
#141422=LINE ( 'NONE', #126956, #32624 ) ;
#141423=DIRECTION ( 'NONE',  ( -0.3543493200069162685, -0.000000000000000000, -0.9351131265310288487 ) ) ;
#141424=DIRECTION ( 'NONE',  ( 0.7071067811865487940, -0.7071067811865463515, 0.000000000000000000 ) ) ;
#141426=VERTEX_POINT ( 'NONE', #34461 ) ;
#141428=CARTESIAN_POINT ( 'NONE',  ( -15.63964197871511885, 8.074661077379714058, 4.334728602384618767 ) ) ;
#141430=CARTESIAN_POINT ( 'NONE',  ( -8.999999999999941380, -13.06887692260767686, 4.000000000000000000 ) ) ;
#141431=CARTESIAN_POINT ( 'NONE',  ( 34.42499999999998295, 22.22500000000000142, 4.165035510187007795 ) ) ;
#141432=DIRECTION ( 'NONE',  ( -0.000000000000000000, 0.000000000000000000, 1.000000000000000000 ) ) ;
#141434=CARTESIAN_POINT ( 'NONE',  ( -74.99451991528749772, 28.92564299267990435, 4.000000000000000000 ) ) ;
#141435=EDGE_CURVE ( 'NONE', #74099, #136109, #56958, .T. ) ;
#141437=EDGE_LOOP ( 'NONE', ( #104469, #134012, #92170, #23710, #28686 ) ) ;
#141438=ORIENTED_EDGE ( 'NONE', *, *, #112131, .T. ) ;
#141440=ORIENTED_EDGE ( 'NONE', *, *, #128754, .T. ) ;
#141441=VECTOR ( 'NONE', #77663, 1000.000000000000000 ) ;
#141442=LINE ( 'NONE', #96468, #66855 ) ;
#141444=VECTOR ( 'NONE', #57082, 1000.000000000000000 ) ;
#141445=CARTESIAN_POINT ( 'NONE',  ( -34.92500000000001137, 21.72500000000000142, 5.000000000000000000 ) ) ;
#141446=LINE ( 'NONE', #118235, #59621 ) ;
#141448=CARTESIAN_POINT ( 'NONE',  ( 45.18398860626900415, 28.73617430169818832, 5.000000000000000000 ) ) ;
#141449=AXIS2_PLACEMENT_3D ( 'NONE', #105279, #53025, #86406 ) ;
#141450=AXIS2_PLACEMENT_3D ( 'NONE', #37327, #59801, #27145 ) ;
#141452=ORIENTED_EDGE ( 'NONE', *, *, #75018, .T. ) ;
#141453=EDGE_CURVE ( 'NONE', #124154, #31469, #11239, .T. ) ;
#141454=VECTOR ( 'NONE', #68096, 1000.000000000000227 ) ;
#141456=ORIENTED_EDGE ( 'NONE', *, *, #142187, .F. ) ;
#141457=DIRECTION ( 'NONE',  ( 0.7071067811865487940, -0.7071067811865463515, 0.000000000000000000 ) ) ;
#141460=LINE ( 'NONE', #130603, #71912 ) ;
#141462=VERTEX_POINT ( 'NONE', #102591 ) ;
#141466=CARTESIAN_POINT ( 'NONE',  ( -18.79289321881331887, -5.240707523384230626, 5.000000000000000000 ) ) ;
#141467=CARTESIAN_POINT ( 'NONE',  ( 13.17183060077638324, -17.24070752338410628, 4.000000000000000000 ) ) ;
#141468=DIRECTION ( 'NONE',  ( 0.000000000000000000, 0.000000000000000000, -1.000000000000000000 ) ) ;
#141469=DIRECTION ( 'NONE',  ( -0.000000000000000000, -0.3543493200069152693, 0.9351131265310292928 ) ) ;
#141470=VECTOR ( 'NONE', #90296, 999.9999999999998863 ) ;
#141473=DIRECTION ( 'NONE',  ( -0.7071067811865486830, -0.7071067811865464625, -0.000000000000000000 ) ) ;
#141474=ORIENTED_EDGE ( 'NONE', *, *, #37313, .T. ) ;
#141475=VERTEX_POINT ( 'NONE', #1776 ) ;
#141476=VECTOR ( 'NONE', #97743, 1000.000000000000227 ) ;
#141477=ORIENTED_EDGE ( 'NONE', *, *, #1841, .F. ) ;
#141478=VECTOR ( 'NONE', #84006, 999.9999999999998863 ) ;
#141481=ORIENTED_EDGE ( 'NONE', *, *, #23700, .F. ) ;
#141483=AXIS2_PLACEMENT_3D ( 'NONE', #110655, #53459, #133877 ) ;
#141484=DIRECTION ( 'NONE',  ( -0.3543493200069162685, -0.000000000000000000, -0.9351131265310288487 ) ) ;
#141486=DIRECTION ( 'NONE',  ( -0.7071067811865486830, 0.7071067811865464625, 0.000000000000000000 ) ) ;
#141487=EDGE_CURVE ( 'NONE', #142366, #63264, #28595, .T. ) ;
#141488=FACE_BOUND ( 'NONE', #28564, .T. ) ;
#141489=VERTEX_POINT ( 'NONE', #93126 ) ;
#141490=CARTESIAN_POINT ( 'NONE',  ( 48.48921356237309510, -27.52281430457089328, 5.000000000000000000 ) ) ;
#141492=DIRECTION ( 'NONE',  ( -1.000000000000000000, 0.000000000000000000, -0.000000000000000000 ) ) ;
#141493=EDGE_CURVE ( 'NONE', #56410, #28809, #74570, .T. ) ;
#141494=EDGE_LOOP ( 'NONE', ( #1377, #59595, #66911, #75225 ) ) ;
#141496=CARTESIAN_POINT ( 'NONE',  ( -22.62823445044371340, -8.240707523384196875, 11.38925528200757853 ) ) ;
#141497=ORIENTED_EDGE ( 'NONE', *, *, #116409, .F. ) ;
#141498=ORIENTED_EDGE ( 'NONE', *, *, #103325, .T. ) ;
#141499=VECTOR ( 'NONE', #74585, 1000.000000000000000 ) ;
#141500=LINE ( 'NONE', #138656, #95776 ) ;
#141501=ORIENTED_EDGE ( 'NONE', *, *, #13305, .F. ) ;
#141503=EDGE_LOOP ( 'NONE', ( #26581, #59175, #33587, #26971 ) ) ;
#141504=PLANE ( 'NONE',  #136670 ) ;
#141505=DIRECTION ( 'NONE',  ( 0.6830127018922181881, 0.6830127018922202975, -0.2588190451025214056 ) ) ;
#141506=ORIENTED_EDGE ( 'NONE', *, *, #5818, .F. ) ;
#141507=LINE ( 'NONE', #19008, #60786 ) ;
#141508=DIRECTION ( 'NONE',  ( -0.7071067811865486830, -0.7071067811865464625, 0.000000000000000000 ) ) ;
#141509=AXIS2_PLACEMENT_3D ( 'NONE', #50088, #127641, #18111 ) ;
#141510=ADVANCED_FACE ( 'NONE', ( #72852 ), #14837, .F. ) ;
#141511=VECTOR ( 'NONE', #85874, 1000.000000000000000 ) ;
#141512=VECTOR ( 'NONE', #70207, 999.9999999999998863 ) ;
#141513=DIRECTION ( 'NONE',  ( 0.7071067811865487940, 0.7071067811865463515, 0.000000000000000000 ) ) ;
#141515=CARTESIAN_POINT ( 'NONE',  ( 12.47336096364207236, -5.240707523384232402, 16.25846745537498705 ) ) ;
#141516=CARTESIAN_POINT ( 'NONE',  ( -28.17183060077627843, 21.75929247661548871, 4.000000000000000000 ) ) ;
#141517=ORIENTED_EDGE ( 'NONE', *, *, #85912, .T. ) ;
#141519=VECTOR ( 'NONE', #53895, 1000.000000000000000 ) ;
#141520=ORIENTED_EDGE ( 'NONE', *, *, #83733, .T. ) ;
#141522=EDGE_LOOP ( 'NONE', ( #104717, #16333, #92919, #105274 ) ) ;
#141524=DIRECTION ( 'NONE',  ( 1.000000000000000000, 0.000000000000000000, 0.000000000000000000 ) ) ;
#141525=ORIENTED_EDGE ( 'NONE', *, *, #13037, .T. ) ;
#141526=VECTOR ( 'NONE', #63301, 999.9999999999998863 ) ;
#141527=ORIENTED_EDGE ( 'NONE', *, *, #96017, .T. ) ;
#141528=VERTEX_POINT ( 'NONE', #15517 ) ;
#141529=CARTESIAN_POINT ( 'NONE',  ( -26.20666063542134339, 21.75929247661549226, 4.998822639870711626 ) ) ;
#141531=CARTESIAN_POINT ( 'NONE',  ( -28.82816939922333432, -5.240707523384228850, 4.000000000000000000 ) ) ;
#141532=ORIENTED_EDGE ( 'NONE', *, *, #67925, .F. ) ;
#141533=VECTOR ( 'NONE', #13391, 999.9999999999998863 ) ;
#141534=CARTESIAN_POINT ( 'NONE',  ( 34.92499999999998295, -21.72500000000000142, 5.000000000000000000 ) ) ;
#141535=CARTESIAN_POINT ( 'NONE',  ( 30.18398860626900060, 28.73617430169808173, 5.000000000000000000 ) ) ;
#141537=EDGE_CURVE ( 'NONE', #11432, #77500, #117006, .T. ) ;
#141538=CARTESIAN_POINT ( 'NONE',  ( -68.99451991528748351, 28.92564299267986172, 4.000000000000000000 ) ) ;
#141539=ORIENTED_EDGE ( 'NONE', *, *, #59651, .T. ) ;
#141542=EDGE_CURVE ( 'NONE', #83949, #72597, #116297, .T. ) ;
#141543=DIRECTION ( 'NONE',  ( 0.7071067811865487940, 0.7071067811865463515, 0.000000000000000000 ) ) ;
#141544=DIRECTION ( 'NONE',  ( -0.6830127018922180770, -0.6830127018922204085, -0.2588190451025213501 ) ) ;
#141545=CARTESIAN_POINT ( 'NONE',  ( -4.190466188707369533, -22.22500000000000142, -6.646463778304954495 ) ) ;
#141546=VERTEX_POINT ( 'NONE', #3916 ) ;
#141547=DIRECTION ( 'NONE',  ( -0.7071067811865487940, 0.7071067811865463515, -0.000000000000000000 ) ) ;
#141548=ORIENTED_EDGE ( 'NONE', *, *, #52920, .T. ) ;
#141549=CARTESIAN_POINT ( 'NONE',  ( -23.24240614354803824, -1.100504885936601784, 4.183743008713593170 ) ) ;
#141550=FACE_OUTER_BOUND ( 'NONE', #79474, .T. ) ;
#141551=ADVANCED_FACE ( 'NONE', ( #6066 ), #39475, .F. ) ;
#141552=ADVANCED_FACE ( 'NONE', ( #103965 ), #61947, .F. ) ;
#141553=DIRECTION ( 'NONE',  ( 0.7071067811865487940, 0.7071067811865463515, -0.000000000000000000 ) ) ;
#141554=VERTEX_POINT ( 'NONE', #83710 ) ;
#141556=VECTOR ( 'NONE', #110752, 1000.000000000000227 ) ;
#141557=CIRCLE ( 'NONE', #79091, 5.968999999999998529 ) ;
#141558=CARTESIAN_POINT ( 'NONE',  ( 34.92499999999998295, -21.72500000000000142, 5.000000000000000000 ) ) ;
#141560=EDGE_LOOP ( 'NONE', ( #20816, #98235, #54078, #87483 ) ) ;
#141561=DIRECTION ( 'NONE',  ( 0.7071067811865486830, -0.7071067811865464625, -0.000000000000000000 ) ) ;
#141562=VECTOR ( 'NONE', #78135, 1000.000000000000227 ) ;
#141563=DIRECTION ( 'NONE',  ( 0.3543493200069162685, -0.000000000000000000, -0.9351131265310288487 ) ) ;
#141564=VERTEX_POINT ( 'NONE', #48193 ) ;
#141566=EDGE_CURVE ( 'NONE', #95511, #5654, #135912, .T. ) ;
#141567=CARTESIAN_POINT ( 'NONE',  ( 20.50183651486031522, -17.24070752338409918, 8.407044977365179861 ) ) ;
#141568=ORIENTED_EDGE ( 'NONE', *, *, #25026, .T. ) ;
#141570=ADVANCED_FACE ( 'NONE', ( #104705 ), #80839, .F. ) ;
#141571=ORIENTED_EDGE ( 'NONE', *, *, #115107, .T. ) ;
#141572=DIRECTION ( 'NONE',  ( 0.7071067811865487940, 0.7071067811865463515, -0.000000000000000000 ) ) ;
#141574=EDGE_CURVE ( 'NONE', #37037, #16100, #26441, .T. ) ;
#141577=DIRECTION ( 'NONE',  ( -0.7071067811865486830, 0.7071067811865464625, 0.000000000000000000 ) ) ;
#141579=ORIENTED_EDGE ( 'NONE', *, *, #124012, .T. ) ;
#141580=LINE ( 'NONE', #120484, #58328 ) ;
#141581=CARTESIAN_POINT ( 'NONE',  ( -12.70710678118645376, 20.25929247661551713, 5.000000000000000000 ) ) ;
#141582=ADVANCED_FACE ( 'NONE', ( #127164 ), #61264, .T. ) ;
#141583=VECTOR ( 'NONE', #50121, 1000.000000000000227 ) ;
#141586=CARTESIAN_POINT ( 'NONE',  ( 14.99451991528749595, 28.92564299267948513, 4.000000000000000000 ) ) ;
#141587=ORIENTED_EDGE ( 'NONE', *, *, #132508, .T. ) ;
#141588=LINE ( 'NONE', #72811, #65014 ) ;
#141589=ORIENTED_EDGE ( 'NONE', *, *, #58693, .T. ) ;
#141590=ORIENTED_EDGE ( 'NONE', *, *, #81334, .F. ) ;
#141591=EDGE_CURVE ( 'NONE', #16744, #48450, #137355, .T. ) ;
#141592=LINE ( 'NONE', #146, #47977 ) ;
#141593=DIRECTION ( 'NONE',  ( 0.6830127018922181881, 0.6830127018922202975, -0.2588190451025214056 ) ) ;
#141594=ORIENTED_EDGE ( 'NONE', *, *, #115932, .T. ) ;
#141595=LINE ( 'NONE', #130736, #122606 ) ;
#141596=FACE_OUTER_BOUND ( 'NONE', #54017, .T. ) ;
#141597=CARTESIAN_POINT ( 'NONE',  ( -51.29974487139158867, -27.71228299555242103, 4.000000000000000000 ) ) ;
#141599=DIRECTION ( 'NONE',  ( 0.7071067811865487940, 0.7071067811865463515, 0.000000000000000000 ) ) ;
#141601=ADVANCED_FACE ( 'NONE', ( #38046 ), #138784, .T. ) ;
#141602=DIRECTION ( 'NONE',  ( -0.000000000000000000, 0.000000000000000000, 1.000000000000000000 ) ) ;
#141604=ADVANCED_FACE ( 'NONE', ( #27141 ), #49653, .F. ) ;
#141605=CARTESIAN_POINT ( 'NONE',  ( 60.29974487139158867, -27.71228299555248142, 4.000000000000000000 ) ) ;
#141608=PLANE ( 'NONE',  #137041 ) ;
#141609=DIRECTION ( 'NONE',  ( -0.7071067811865487940, 0.7071067811865463515, 0.000000000000000000 ) ) ;
#141611=ADVANCED_FACE ( 'NONE', ( #40205 ), #128608, .F. ) ;
#141612=DIRECTION ( 'NONE',  ( -0.000000000000000000, 0.000000000000000000, 1.000000000000000000 ) ) ;
#141613=VERTEX_POINT ( 'NONE', #119834 ) ;
#141614=VERTEX_POINT ( 'NONE', #52455 ) ;
#141616=CARTESIAN_POINT ( 'NONE',  ( 9.489213562373095101, -27.52281430457062328, 5.000000000000000000 ) ) ;
#141617=LINE ( 'NONE', #98110, #25347 ) ;
#141618=LINE ( 'NONE', #77098, #53047 ) ;
#141619=ORIENTED_EDGE ( 'NONE', *, *, #118743, .T. ) ;
#141620=VECTOR ( 'NONE', #73793, 1000.000000000000000 ) ;
#141621=AXIS2_PLACEMENT_3D ( 'NONE', #140625, #137805, #84834 ) ;
#141622=DIRECTION ( 'NONE',  ( 0.7071067811865486830, -0.7071067811865464625, -0.000000000000000000 ) ) ;
#141623=VECTOR ( 'NONE', #105309, 999.9999999999998863 ) ;
#141625=ORIENTED_EDGE ( 'NONE', *, *, #104869, .F. ) ;
#141626=CARTESIAN_POINT ( 'NONE',  ( 5.999999999999960032, -11.35517001088072142, -1.126524801160094347 ) ) ;
#141627=VERTEX_POINT ( 'NONE', #108233 ) ;
#141628=VECTOR ( 'NONE', #62958, 1000.000000000000000 ) ;
#141629=EDGE_LOOP ( 'NONE', ( #71321, #60823, #1575 ) ) ;
#141631=VECTOR ( 'NONE', #125179, 1000.000000000000000 ) ;
#141632=VECTOR ( 'NONE', #38232, 1000.000000000000114 ) ;
#141633=CARTESIAN_POINT ( 'NONE',  ( 5.510786437626906675, -27.52281430457051314, 5.000000000000000000 ) ) ;
#141634=VECTOR ( 'NONE', #126653, 1000.000000000000000 ) ;
#141635=LINE ( 'NONE', #74968, #80118 ) ;
#141636=DIRECTION ( 'NONE',  ( -0.000000000000000000, -0.3543493200069152693, 0.9351131265310292928 ) ) ;
#141637=DIRECTION ( 'NONE',  ( -0.000000000000000000, 0.000000000000000000, 1.000000000000000000 ) ) ;
#141638=EDGE_LOOP ( 'NONE', ( #59792, #80016, #94522, #75108, #140386 ) ) ;
#141639=DIRECTION ( 'NONE',  ( 0.6830127018922181881, 0.6830127018922202975, -0.2588190451025214056 ) ) ;
#141641=ORIENTED_EDGE ( 'NONE', *, *, #53404, .T. ) ;
#141644=CARTESIAN_POINT ( 'NONE',  ( 14.51078643762690490, -27.52281430457045275, 5.000000000000000000 ) ) ;
#141647=CARTESIAN_POINT ( 'NONE',  ( -4.446650576632151797, 2.259292476615694323, 14.86850063742355488 ) ) ;
#141648=PLANE ( 'NONE',  #92442 ) ;
#141652=CARTESIAN_POINT ( 'NONE',  ( -21.00548008471250938, 28.92564299267923644, 4.000000000000000000 ) ) ;
#141653=DIRECTION ( 'NONE',  ( -0.7071067811865486830, -0.7071067811865464625, 0.000000000000000000 ) ) ;
#141654=DIRECTION ( 'NONE',  ( -0.7071067811865487940, 0.7071067811865463515, -0.000000000000000000 ) ) ;
#141655=VERTEX_POINT ( 'NONE', #118428 ) ;
#141656=EDGE_LOOP ( 'NONE', ( #90298, #64281, #142348, #5246 ) ) ;
#141657=CARTESIAN_POINT ( 'NONE',  ( -18.85181644961843972, 17.25929247661554555, 8.802941693769158249 ) ) ;
#141658=DIRECTION ( 'NONE',  ( 0.000000000000000000, 0.000000000000000000, 1.000000000000000000 ) ) ;
#141660=VECTOR ( 'NONE', #37561, 1000.000000000000000 ) ;
#141661=ORIENTED_EDGE ( 'NONE', *, *, #100711, .F. ) ;
#141662=VECTOR ( 'NONE', #85830, 1000.000000000000000 ) ;
#141664=EDGE_LOOP ( 'NONE', ( #96466, #20925, #21266, #86943 ) ) ;
#141665=VECTOR ( 'NONE', #43463, 999.9999999999998863 ) ;
#141666=LINE ( 'NONE', #216, #111701 ) ;
#141667=DIRECTION ( 'NONE',  ( -0.6830127018922181881, 0.6830127018922202975, -0.2588190451025214056 ) ) ;
#141668=EDGE_CURVE ( 'NONE', #80500, #33114, #131469, .T. ) ;
#141669=FACE_BOUND ( 'NONE', #56563, .T. ) ;
#141670=DIRECTION ( 'NONE',  ( -0.3543493200069162685, -0.000000000000000000, -0.9351131265310288487 ) ) ;
#141671=CARTESIAN_POINT ( 'NONE',  ( -17.81601139373099940, 28.73617430169775133, 5.000000000000000000 ) ) ;
#141672=EDGE_CURVE ( 'NONE', #68801, #69641, #95963, .T. ) ;
#141675=ORIENTED_EDGE ( 'NONE', *, *, #30775, .F. ) ;
#141676=AXIS2_PLACEMENT_3D ( 'NONE', #43093, #85857, #119886 ) ;
#141677=CARTESIAN_POINT ( 'NONE',  ( 6.183988606268994381, 28.73617430169791476, 5.000000000000000000 ) ) ;
#141678=ORIENTED_EDGE ( 'NONE', *, *, #4143, .F. ) ;
#141679=ORIENTED_EDGE ( 'NONE', *, *, #108266, .T. ) ;
#141681=VERTEX_POINT ( 'NONE', #64787 ) ;
#141682=DIRECTION ( 'NONE',  ( -0.7071067811865486830, 0.7071067811865463515, 0.000000000000000000 ) ) ;
#141683=ADVANCED_FACE ( 'NONE', ( #129300 ), #63388, .T. ) ;
#141684=DIRECTION ( 'NONE',  ( -0.6830127018922180770, -0.6830127018922204085, -0.2588190451025213501 ) ) ;
#141687=CARTESIAN_POINT ( 'NONE',  ( -14.81601139373099585, 28.73617430169776910, 5.000000000000000000 ) ) ;
#141690=FACE_OUTER_BOUND ( 'NONE', #49744, .T. ) ;
#141691=CARTESIAN_POINT ( 'NONE',  ( -4.499999999999962697, -7.420205493532904484, -2.617629953481263261 ) ) ;
#141692=LINE ( 'NONE', #42395, #131160 ) ;
#141693=FACE_OUTER_BOUND ( 'NONE', #139814, .T. ) ;
#141694=CARTESIAN_POINT ( 'NONE',  ( 20.12514619309222041, -14.24070752338413470, 9.401115078912612333 ) ) ;
#141695=DIRECTION ( 'NONE',  ( -0.7071067811865487940, 0.7071067811865463515, 0.000000000000000000 ) ) ;
#141696=PLANE ( 'NONE',  #25391 ) ;
#141697=ORIENTED_EDGE ( 'NONE', *, *, #25696, .T. ) ;
#141698=VECTOR ( 'NONE', #8828, 1000.000000000000227 ) ;
#141699=EDGE_CURVE ( 'NONE', #121031, #55582, #86545, .T. ) ;
#141700=CARTESIAN_POINT ( 'NONE',  ( -19.82816939922339117, -5.240707523384228850, 4.000000000000000000 ) ) ;
#141701=ORIENTED_EDGE ( 'NONE', *, *, #120189, .F. ) ;
#141702=LINE ( 'NONE', #1675, #102828 ) ;
#141703=DIRECTION ( 'NONE',  ( -0.6830127018922180770, -0.6830127018922204085, -0.2588190451025213501 ) ) ;
#141704=VERTEX_POINT ( 'NONE', #41584 ) ;
#141705=ORIENTED_EDGE ( 'NONE', *, *, #87527, .T. ) ;
#141706=ORIENTED_EDGE ( 'NONE', *, *, #72711, .T. ) ;
#141708=VECTOR ( 'NONE', #113585, 1000.000000000000227 ) ;
#141709=ORIENTED_EDGE ( 'NONE', *, *, #92270, .T. ) ;
#141710=CARTESIAN_POINT ( 'NONE',  ( -4.499999999999976019, 22.22500000000000142, 4.362957392718799454 ) ) ;
#141711=CARTESIAN_POINT ( 'NONE',  ( -14.29289321881335262, -15.74070752338412760, 5.000000000000000000 ) ) ;
#141714=ORIENTED_EDGE ( 'NONE', *, *, #71373, .F. ) ;
#141716=EDGE_CURVE ( 'NONE', #137834, #74547, #18376, .T. ) ;
#141717=ORIENTED_EDGE ( 'NONE', *, *, #134166, .F. ) ;
#141718=CARTESIAN_POINT ( 'NONE',  ( -3.489213562373097322, -27.52281430457057709, 5.000000000000000000 ) ) ;
#141719=CARTESIAN_POINT ( 'NONE',  ( -34.92500000000001137, -16.29806943317882073, 4.500000000000000888 ) ) ;
#141720=AXIS2_PLACEMENT_3D ( 'NONE', #29932, #106777, #53869 ) ;
#141722=LINE ( 'NONE', #54717, #56419 ) ;
#141723=ORIENTED_EDGE ( 'NONE', *, *, #36295, .F. ) ;
#141724=VECTOR ( 'NONE', #31114, 1000.000000000000000 ) ;
#141725=VERTEX_POINT ( 'NONE', #85803 ) ;
#141726=CARTESIAN_POINT ( 'NONE',  ( -23.20710678118637915, -20.24070752338406720, 5.000000000000000000 ) ) ;
#141727=LINE ( 'NONE', #32240, #107038 ) ;
#141728=EDGE_CURVE ( 'NONE', #94372, #131124, #107554, .T. ) ;
#141730=EDGE_CURVE ( 'NONE', #102027, #67530, #139521, .T. ) ;
#141731=FACE_OUTER_BOUND ( 'NONE', #88772, .T. ) ;
#141733=ORIENTED_EDGE ( 'NONE', *, *, #66273, .T. ) ;
#141734=CARTESIAN_POINT ( 'NONE',  ( -3.489213562373097322, -27.52281430457057709, 5.000000000000000000 ) ) ;
#141738=DIRECTION ( 'NONE',  ( -0.6830127018922181881, 0.6830127018922202975, -0.2588190451025214056 ) ) ;
#141739=VECTOR ( 'NONE', #94685, 1000.000000000000000 ) ;
#141742=DIRECTION ( 'NONE',  ( -0.7071067811865486830, 0.7071067811865464625, 0.000000000000000000 ) ) ;
#141744=LINE ( 'NONE', #77902, #28453 ) ;
#141745=CARTESIAN_POINT ( 'NONE',  ( 66.48921356237309510, -27.52281430457101763, 5.000000000000000000 ) ) ;
#141747=EDGE_CURVE ( 'NONE', #98173, #8470, #7517, .T. ) ;
#141748=CARTESIAN_POINT ( 'NONE',  ( -31.49999999999977263, 13.08746187583910370, 4.000000000000000000 ) ) ;
#141749=EDGE_LOOP ( 'NONE', ( #39949, #38298, #82358, #112614 ) ) ;
#141750=ADVANCED_FACE ( 'NONE', ( #76375 ), #42334, .F. ) ;
#141751=DIRECTION ( 'NONE',  ( 0.7071067811865486830, -0.7071067811865464625, -0.000000000000000000 ) ) ;
#141752=ORIENTED_EDGE ( 'NONE', *, *, #131029, .F. ) ;
#141753=DIRECTION ( 'NONE',  ( 0.3543493200069162685, -0.000000000000000000, -0.9351131265310288487 ) ) ;
#141755=ORIENTED_EDGE ( 'NONE', *, *, #113630, .F. ) ;
#141756=CARTESIAN_POINT ( 'NONE',  ( 0.000000000000000000, 0.000000000000000000, 5.000000000000000000 ) ) ;
#141757=EDGE_CURVE ( 'NONE', #17670, #91794, #130774, .T. ) ;
#141759=ORIENTED_EDGE ( 'NONE', *, *, #105818, .T. ) ;
#141760=ORIENTED_EDGE ( 'NONE', *, *, #98301, .T. ) ;
#141762=CARTESIAN_POINT ( 'NONE',  ( -29.21837311707484730, 21.74787736706806740, 4.999607392498049308 ) ) ;
#141763=LINE ( 'NONE', #51898, #30722 ) ;
#141765=EDGE_CURVE ( 'NONE', #14410, #45511, #106099, .T. ) ;
#141766=LINE ( 'NONE', #55464, #106057 ) ;
#141768=VECTOR ( 'NONE', #58840, 1000.000000000000000 ) ;
#141769=DIRECTION ( 'NONE',  ( -0.3543493200069162685, -0.000000000000000000, -0.9351131265310288487 ) ) ;
#141770=AXIS2_PLACEMENT_3D ( 'NONE', #50203, #138635, #105962 ) ;
#141771=CARTESIAN_POINT ( 'NONE',  ( 45.48921356237309510, -27.52281430457087197, 5.000000000000000000 ) ) ;
#141772=CARTESIAN_POINT ( 'NONE',  ( -30.29974487139158867, -27.71228299555227537, 4.000000000000000000 ) ) ;
#141773=CARTESIAN_POINT ( 'NONE',  ( 12.48921356237309155, -27.52281430457064104, 5.000000000000000000 ) ) ;
#141774=ORIENTED_EDGE ( 'NONE', *, *, #427, .T. ) ;
#141775=LINE ( 'NONE', #65673, #72035 ) ;
#141776=ORIENTED_EDGE ( 'NONE', *, *, #24175, .F. ) ;
#141778=VECTOR ( 'NONE', #73343, 1000.000000000000000 ) ;
#141779=VERTEX_POINT ( 'NONE', #43041 ) ;
#141780=DIRECTION ( 'NONE',  ( -0.7071067811865487940, 0.7071067811865463515, 0.000000000000000000 ) ) ;
#141782=VERTEX_POINT ( 'NONE', #29282 ) ;
#141784=LINE ( 'NONE', #109843, #18525 ) ;
#141785=CARTESIAN_POINT ( 'NONE',  ( 17.99999999999988276, 11.58746187583911968, 4.000000000000000000 ) ) ;
#141786=ORIENTED_EDGE ( 'NONE', *, *, #47022, .T. ) ;
#141787=EDGE_LOOP ( 'NONE', ( #39843, #3483, #67732 ) ) ;
#141788=DIRECTION ( 'NONE',  ( 0.7071067811865487940, -0.7071067811865463515, 0.000000000000000000 ) ) ;
#141790=VECTOR ( 'NONE', #44359, 1000.000000000000000 ) ;
#141792=CARTESIAN_POINT ( 'NONE',  ( 30.85005128541006059, -8.240707523384196875, 17.25253755692246571 ) ) ;
#141793=EDGE_CURVE ( 'NONE', #143369, #59118, #73524, .T. ) ;
#141796=EDGE_CURVE ( 'NONE', #62769, #119974, #33605, .T. ) ;
#141797=CARTESIAN_POINT ( 'NONE',  ( 30.48921356237309510, -27.52281430457076894, 5.000000000000000000 ) ) ;
#141798=ORIENTED_EDGE ( 'NONE', *, *, #48064, .T. ) ;
#141799=ADVANCED_FACE ( 'NONE', ( #34291 ), #54628, .F. ) ;
#141800=CARTESIAN_POINT ( 'NONE',  ( 30.18398860626900060, 28.73617430169808173, 5.000000000000000000 ) ) ;
#141801=PLANE ( 'NONE',  #27616 ) ;
#141802=CARTESIAN_POINT ( 'NONE',  ( 13.75179860200718984, 5.925774409307370760, 4.669108085256723939 ) ) ;
#141804=VECTOR ( 'NONE', #63542, 999.9999999999998863 ) ;
#141805=VERTEX_POINT ( 'NONE', #101679 ) ;
#141806=DIRECTION ( 'NONE',  ( 0.7071067811865487940, 0.7071067811865463515, 0.000000000000000000 ) ) ;
#141807=VERTEX_POINT ( 'NONE', #66220 ) ;
#141810=DIRECTION ( 'NONE',  ( 0.6830127018922181881, 0.6830127018922202975, -0.2588190451025214056 ) ) ;
#141812=EDGE_LOOP ( 'NONE', ( #112673, #39009, #79160, #7682 ) ) ;
#141813=VECTOR ( 'NONE', #97012, 1000.000000000000000 ) ;
#141814=PLANE ( 'NONE',  #7103 ) ;
#141815=PLANE ( 'NONE',  #7165 ) ;
#141816=DIRECTION ( 'NONE',  ( -0.7071067811865487940, 0.7071067811865463515, -0.000000000000000000 ) ) ;
#141818=DIRECTION ( 'NONE',  ( -0.6830127018922181881, 0.6830127018922202975, -0.2588190451025214056 ) ) ;
#141819=ORIENTED_EDGE ( 'NONE', *, *, #124443, .F. ) ;
#141820=CARTESIAN_POINT ( 'NONE',  ( -30.18398860626900060, 28.73617430169808173, 5.000000000000000000 ) ) ;
#141822=VECTOR ( 'NONE', #15330, 999.9999999999998863 ) ;
#141825=ORIENTED_EDGE ( 'NONE', *, *, #92398, .F. ) ;
#141826=ORIENTED_EDGE ( 'NONE', *, *, #77626, .F. ) ;
#141828=EDGE_LOOP ( 'NONE', ( #88946, #183, #28883, #124545 ) ) ;
#141829=DIRECTION ( 'NONE',  ( -0.000000000000000000, -0.3543493200069152693, 0.9351131265310292928 ) ) ;
#141830=LINE ( 'NONE', #97578, #85081 ) ;
#141831=EDGE_CURVE ( 'NONE', #106541, #2749, #35762, .T. ) ;
#141833=CARTESIAN_POINT ( 'NONE',  ( 22.49999999999985079, -8.947814304570739452, 5.000000000000000000 ) ) ;
#141834=ORIENTED_EDGE ( 'NONE', *, *, #41560, .T. ) ;
#141835=VECTOR ( 'NONE', #118738, 1000.000000000000000 ) ;
#141837=VECTOR ( 'NONE', #100992, 1000.000000000000000 ) ;
#141838=LINE ( 'NONE', #42534, #74633 ) ;
#141840=VECTOR ( 'NONE', #23666, 1000.000000000000000 ) ;
#141841=VERTEX_POINT ( 'NONE', #77115 ) ;
#141842=CARTESIAN_POINT ( 'NONE',  ( -38.99451991528749062, 28.92564299267965211, 4.000000000000000000 ) ) ;
#141843=VECTOR ( 'NONE', #5185, 1000.000000000000000 ) ;
#141844=LINE ( 'NONE', #131672, #8413 ) ;
#141845=PLANE ( 'NONE',  #123399 ) ;
#141848=ORIENTED_EDGE ( 'NONE', *, *, #30080, .T. ) ;
#141849=VERTEX_POINT ( 'NONE', #134331 ) ;
#141851=EDGE_CURVE ( 'NONE', #62501, #130662, #111104, .T. ) ;
#141852=EDGE_CURVE ( 'NONE', #103011, #61774, #99518, .T. ) ;
#141853=DIRECTION ( 'NONE',  ( 0.6830127018922180770, -0.6830127018922204085, -0.2588190451025213501 ) ) ;
#141855=CARTESIAN_POINT ( 'NONE',  ( 25.49999999999982236, 22.01701374228157349, 2.453858888625571666 ) ) ;
#141856=PLANE ( 'NONE',  #133978 ) ;
#141857=DIRECTION ( 'NONE',  ( -0.7071067811865486830, -0.7071067811865464625, 0.000000000000000000 ) ) ;
#141858=EDGE_CURVE ( 'NONE', #114427, #54563, #100964, .T. ) ;
#141859=EDGE_CURVE ( 'NONE', #122401, #85531, #111392, .T. ) ;
#141861=ORIENTED_EDGE ( 'NONE', *, *, #136469, .T. ) ;
#141862=AXIS2_PLACEMENT_3D ( 'NONE', #64192, #43160, #84529 ) ;
#141865=EDGE_LOOP ( 'NONE', ( #33432, #19854, #34442, #1915 ) ) ;
#141869=VECTOR ( 'NONE', #53626, 1000.000000000000000 ) ;
#141870=FACE_OUTER_BOUND ( 'NONE', #31611, .T. ) ;
#141871=EDGE_CURVE ( 'NONE', #57727, #55777, #923, .T. ) ;
#141872=LINE ( 'NONE', #131691, #54151 ) ;
#141873=ORIENTED_EDGE ( 'NONE', *, *, #80983, .T. ) ;
#141875=LINE ( 'NONE', #73730, #95756 ) ;
#141876=AXIS2_PLACEMENT_3D ( 'NONE', #118532, #107651, #8311 ) ;
#141877=DIRECTION ( 'NONE',  ( 0.7071067811865487940, 0.7071067811865463515, 0.000000000000000000 ) ) ;
#141882=EDGE_CURVE ( 'NONE', #23510, #17946, #2337, .T. ) ;
#141883=CARTESIAN_POINT ( 'NONE',  ( 24.48921356237309510, -27.52281430457072631, 5.000000000000000000 ) ) ;
#141884=ORIENTED_EDGE ( 'NONE', *, *, #9594, .F. ) ;
#141885=FACE_OUTER_BOUND ( 'NONE', #129582, .T. ) ;
#141886=CARTESIAN_POINT ( 'NONE',  ( 20.99999999999984723, -16.44781430457065241, 5.000000000000000000 ) ) ;
#141887=ORIENTED_EDGE ( 'NONE', *, *, #8810, .F. ) ;
#141888=DIRECTION ( 'NONE',  ( 0.7071067811865487940, -0.7071067811865463515, 0.000000000000000000 ) ) ;
#141889=VERTEX_POINT ( 'NONE', #112564 ) ;
#141890=ORIENTED_EDGE ( 'NONE', *, *, #26823, .T. ) ;
#141891=VERTEX_POINT ( 'NONE', #87954 ) ;
#141896=CARTESIAN_POINT ( 'NONE',  ( -36.18398860626899705, 28.73617430169812437, 5.000000000000000000 ) ) ;
#141897=PLANE ( 'NONE',  #93654 ) ;
#141899=CARTESIAN_POINT ( 'NONE',  ( -8.999999999999934275, -6.412538124160692909, 4.000000000000000000 ) ) ;
#141900=AXIS2_PLACEMENT_3D ( 'NONE', #112779, #89597, #54855 ) ;
#141901=DIRECTION ( 'NONE',  ( -0.3543493200069162685, -0.000000000000000000, -0.9351131265310288487 ) ) ;
#141902=ADVANCED_FACE ( 'NONE', ( #94368 ), #13939, .F. ) ;
#141903=EDGE_LOOP ( 'NONE', ( #47069, #84798, #83169, #45164 ) ) ;
#141904=DIRECTION ( 'NONE',  ( 0.6830127018922181881, 0.6830127018922202975, -0.2588190451025214056 ) ) ;
#141905=VECTOR ( 'NONE', #64949, 1000.000000000000000 ) ;
#141906=CARTESIAN_POINT ( 'NONE',  ( 12.18398860626900060, 28.73617430169795739, 5.000000000000000000 ) ) ;
#141907=( BOUNDED_CURVE ( )  B_SPLINE_CURVE ( 3, ( #108758, #33424, #77622, #88495 ),
 .UNSPECIFIED., .F., .F. ) 
 B_SPLINE_CURVE_WITH_KNOTS ( ( 4, 4 ),
 ( 5.920967161967926273, 7.341195215986648037 ),
 .UNSPECIFIED. ) 
 CURVE ( )  GEOMETRIC_REPRESENTATION_ITEM ( )  RATIONAL_B_SPLINE_CURVE ( ( 1.000000000000000000, 0.8388583629366588301, 0.8388583629366588301, 1.000000000000000000 ) ) 
 REPRESENTATION_ITEM ( '' )  );
#141911=VERTEX_POINT ( 'NONE', #5905 ) ;
#141912=LINE ( 'NONE', #65800, #113158 ) ;
#141913=ORIENTED_EDGE ( 'NONE', *, *, #43055, .F. ) ;
#141915=VERTEX_POINT ( 'NONE', #83529 ) ;
#141916=ORIENTED_EDGE ( 'NONE', *, *, #23764, .T. ) ;
#141919=EDGE_LOOP ( 'NONE', ( #70237, #26355, #119530, #74730 ) ) ;
#141921=ADVANCED_FACE ( 'NONE', ( #16825 ), #25545, .F. ) ;
#141922=DIRECTION ( 'NONE',  ( -0.7071067811865487940, 0.7071067811865463515, -0.000000000000000000 ) ) ;
#141924=ORIENTED_EDGE ( 'NONE', *, *, #75387, .T. ) ;
#141925=LINE ( 'NONE', #56362, #62753 ) ;
#141926=AXIS2_PLACEMENT_3D ( 'NONE', #102039, #36766, #46265 ) ;
#141927=ORIENTED_EDGE ( 'NONE', *, *, #133989, .F. ) ;
#141929=DIRECTION ( 'NONE',  ( -0.7071067811865486830, -0.7071067811865464625, 0.000000000000000000 ) ) ;
#141931=ADVANCED_FACE ( 'NONE', ( #58240 ), #69817, .F. ) ;
#141932=DIRECTION ( 'NONE',  ( -0.000000000000000000, 0.3543493200069153248, 0.9351131265310292928 ) ) ;
#141934=ORIENTED_EDGE ( 'NONE', *, *, #40080, .T. ) ;
#141935=ORIENTED_EDGE ( 'NONE', *, *, #135180, .T. ) ;
#141937=DIRECTION ( 'NONE',  ( 0.7071067811865487940, 0.7071067811865463515, 0.000000000000000000 ) ) ;
#141938=VECTOR ( 'NONE', #33379, 999.9999999999998863 ) ;
#141941=CARTESIAN_POINT ( 'NONE',  ( -3.707106781186519928, 5.259292476615663681, 5.000000000000000000 ) ) ;
#141942=AXIS2_PLACEMENT_3D ( 'NONE', #105334, #114075, #3159 ) ;
#141943=CARTESIAN_POINT ( 'NONE',  ( 29.99451991528749417, 28.92564299267958816, 4.000000000000000000 ) ) ;
#141944=CARTESIAN_POINT ( 'NONE',  ( -19.05000000000000071, 3.174999999999997158, 1.444000000000000394 ) ) ;
#141947=LINE ( 'NONE', #17278, #16435 ) ;
#141948=ORIENTED_EDGE ( 'NONE', *, *, #72655, .T. ) ;
#141949=DIRECTION ( 'NONE',  ( -0.3543493200069162685, -0.000000000000000000, -0.9351131265310288487 ) ) ;
#141950=VECTOR ( 'NONE', #94441, 1000.000000000000000 ) ;
#141951=VECTOR ( 'NONE', #126963, 1000.000000000000000 ) ;
#141953=FACE_OUTER_BOUND ( 'NONE', #104777, .T. ) ;
#141954=ORIENTED_EDGE ( 'NONE', *, *, #58435, .T. ) ;
#141955=LINE ( 'NONE', #86842, #71515 ) ;
#141956=DIRECTION ( 'NONE',  ( -0.6830127018922180770, -0.6830127018922204085, -0.2588190451025213501 ) ) ;
#141957=ORIENTED_EDGE ( 'NONE', *, *, #136766, .F. ) ;
#141958=LINE ( 'NONE', #21584, #60826 ) ;
#141960=ORIENTED_EDGE ( 'NONE', *, *, #1260, .T. ) ;
#141962=ORIENTED_EDGE ( 'NONE', *, *, #38949, .T. ) ;
#141963=CARTESIAN_POINT ( 'NONE',  ( -12.29974487139158512, -27.71228299555214747, 4.000000000000000000 ) ) ;
#141965=CARTESIAN_POINT ( 'NONE',  ( -26.29289321881326913, 20.25929247661551003, 5.000000000000000000 ) ) ;
#141966=EDGE_CURVE ( 'NONE', #50223, #129671, #26977, .T. ) ;
#141968=LINE ( 'NONE', #86858, #20456 ) ;
#141969=DIRECTION ( 'NONE',  ( -0.6830127018922180770, -0.6830127018922204085, -0.2588190451025213501 ) ) ;
#141971=DIRECTION ( 'NONE',  ( -0.7071067811865487940, 0.7071067811865463515, -0.000000000000000000 ) ) ;
#141975=DIRECTION ( 'NONE',  ( -0.000000000000000000, -0.3543493200069152693, 0.9351131265310292928 ) ) ;
#141976=VERTEX_POINT ( 'NONE', #137903 ) ;
#141978=ORIENTED_EDGE ( 'NONE', *, *, #126649, .T. ) ;
#141979=EDGE_CURVE ( 'NONE', #115599, #69745, #82812, .T. ) ;
#141980=CARTESIAN_POINT ( 'NONE',  ( 0.000000000000000000, 0.000000000000000000, 5.000000000000000000 ) ) ;
#141981=VERTEX_POINT ( 'NONE', #71952 ) ;
#141982=VECTOR ( 'NONE', #115472, 1000.000000000000000 ) ;
#141983=CARTESIAN_POINT ( 'NONE',  ( -63.18398860626900415, 28.73617430169831621, 5.000000000000000000 ) ) ;
#141985=ORIENTED_EDGE ( 'NONE', *, *, #86685, .F. ) ;
#141986=CARTESIAN_POINT ( 'NONE',  ( -1.499999999999985789, -7.533600742197660516, 5.000000000000000000 ) ) ;
#141987=DIRECTION ( 'NONE',  ( 0.6830127018922181881, 0.6830127018922202975, -0.2588190451025214056 ) ) ;
#141988=VECTOR ( 'NONE', #1023, 1000.000000000000000 ) ;
#141989=CARTESIAN_POINT ( 'NONE',  ( -1.214984197241888220, -3.740707523384244837, 15.76143240460123707 ) ) ;
#141990=EDGE_CURVE ( 'NONE', #116759, #75714, #116122, .T. ) ;
#141992=CARTESIAN_POINT ( 'NONE',  ( 42.48921356237308800, -27.52281430457085065, 5.000000000000000000 ) ) ;
#141993=VERTEX_POINT ( 'NONE', #107391 ) ;
#141994=LINE ( 'NONE', #142684, #23499 ) ;
#141995=CARTESIAN_POINT ( 'NONE',  ( 84.29974487139159578, -27.71228299555264840, 4.000000000000000000 ) ) ;
#141996=FACE_OUTER_BOUND ( 'NONE', #18354, .T. ) ;
#141997=DIRECTION ( 'NONE',  ( 0.6830127018922181881, 0.6830127018922202975, -0.2588190451025214056 ) ) ;
#141998=DIRECTION ( 'NONE',  ( 0.7071067811865487940, 0.7071067811865463515, 0.000000000000000000 ) ) ;
#141999=VECTOR ( 'NONE', #123229, 1000.000000000000114 ) ;
#142000=ORIENTED_EDGE ( 'NONE', *, *, #8448, .F. ) ;
#142001=ORIENTED_EDGE ( 'NONE', *, *, #33492, .T. ) ;
#142005=EDGE_LOOP ( 'NONE', ( #24177, #7, #103528, #93188 ) ) ;
#142008=AXIS2_PLACEMENT_3D ( 'NONE', #108220, #94512, #140867 ) ;
#142009=LINE ( 'NONE', #42698, #57028 ) ;
#142010=VERTEX_POINT ( 'NONE', #84253 ) ;
#142011=DIRECTION ( 'NONE',  ( 1.000000000000000000, 0.000000000000000000, 0.000000000000000000 ) ) ;
#142014=ORIENTED_EDGE ( 'NONE', *, *, #55889, .F. ) ;
#142015=DIRECTION ( 'NONE',  ( -0.7071067811865487940, 0.7071067811865463515, 0.000000000000000000 ) ) ;
#142016=EDGE_CURVE ( 'NONE', #111064, #108173, #79262, .T. ) ;
#142017=VECTOR ( 'NONE', #116331, 1000.000000000000000 ) ;
#142020=ORIENTED_EDGE ( 'NONE', *, *, #72189, .T. ) ;
#142021=ORIENTED_EDGE ( 'NONE', *, *, #102084, .F. ) ;
#142023=EDGE_CURVE ( 'NONE', #21869, #2836, #28424, .T. ) ;
#142024=EDGE_CURVE ( 'NONE', #109497, #139229, #19669, .T. ) ;
#142025=EDGE_CURVE ( 'NONE', #20582, #95024, #108071, .T. ) ;
#142026=CARTESIAN_POINT ( 'NONE',  ( 2.999999999999983569, -9.412538124160661823, 4.000000000000000000 ) ) ;
#142029=LINE ( 'NONE', #143424, #110460 ) ;
#142030=FACE_OUTER_BOUND ( 'NONE', #54025, .T. ) ;
#142032=EDGE_CURVE ( 'NONE', #73728, #81832, #42165, .T. ) ;
#142036=CARTESIAN_POINT ( 'NONE',  ( 34.42499999999998295, 0.000000000000000000, 4.500000000000000888 ) ) ;
#142037=EDGE_CURVE ( 'NONE', #84513, #114295, #8741, .T. ) ;
#142038=ORIENTED_EDGE ( 'NONE', *, *, #74006, .F. ) ;
#142039=ORIENTED_EDGE ( 'NONE', *, *, #57796, .T. ) ;
#142040=ADVANCED_FACE ( 'NONE', ( #6602 ), #50884, .F. ) ;
#142041=VECTOR ( 'NONE', #98012, 999.9999999999998863 ) ;
#142043=CARTESIAN_POINT ( 'NONE',  ( 69.48921356237309510, -27.52281430457103895, 5.000000000000000000 ) ) ;
#142045=LINE ( 'NONE', #77507, #131603 ) ;
#142047=LINE ( 'NONE', #76798, #6201 ) ;
#142048=VECTOR ( 'NONE', #84937, 1000.000000000000000 ) ;
#142049=DIRECTION ( 'NONE',  ( 0.7071067811865486830, -0.7071067811865464625, -0.000000000000000000 ) ) ;
#142052=EDGE_CURVE ( 'NONE', #88480, #130600, #141460, .T. ) ;
#142054=ORIENTED_EDGE ( 'NONE', *, *, #13422, .T. ) ;
#142055=DIRECTION ( 'NONE',  ( 0.7071067811865486830, -0.7071067811865464625, -0.000000000000000000 ) ) ;
#142056=ORIENTED_EDGE ( 'NONE', *, *, #664, .F. ) ;
#142057=CARTESIAN_POINT ( 'NONE',  ( -42.29974487139158157, -27.71228299555235708, 4.000000000000000000 ) ) ;
#142058=ORIENTED_EDGE ( 'NONE', *, *, #88400, .T. ) ;
#142059=CARTESIAN_POINT ( 'NONE',  ( 22.04263059361153410, -22.22500000000000142, -16.58716479377923392 ) ) ;
#142060=ORIENTED_EDGE ( 'NONE', *, *, #113230, .T. ) ;
#142061=ORIENTED_EDGE ( 'NONE', *, *, #75095, .F. ) ;
#142062=VECTOR ( 'NONE', #32753, 1000.000000000000000 ) ;
#142063=EDGE_CURVE ( 'NONE', #38177, #3445, #119663, .T. ) ;
#142064=ORIENTED_EDGE ( 'NONE', *, *, #124808, .T. ) ;
#142065=DIRECTION ( 'NONE',  ( 1.000000000000000000, 0.000000000000000000, 0.000000000000000000 ) ) ;
#142066=AXIS2_PLACEMENT_3D ( 'NONE', #128916, #116618, #139835 ) ;
#142067=LINE ( 'NONE', #129013, #25244 ) ;
#142068=CARTESIAN_POINT ( 'NONE',  ( -12.18398860626900060, 28.73617430169795739, 5.000000000000000000 ) ) ;
#142069=CARTESIAN_POINT ( 'NONE',  ( -51.48921356237309510, -27.52281430457091460, 5.000000000000000000 ) ) ;
#142070=CARTESIAN_POINT ( 'NONE',  ( 13.73493329717941158, 12.75929247661558996, 18.34774599283953123 ) ) ;
#142071=CARTESIAN_POINT ( 'NONE',  ( 18.32816939922340183, -3.740707523384248390, 4.000000000000000000 ) ) ;
#142072=AXIS2_PLACEMENT_3D ( 'NONE', #33684, #77885, #43124 ) ;
#142074=LINE ( 'NONE', #39916, #27394 ) ;
#142075=EDGE_CURVE ( 'NONE', #57315, #5353, #102055, .T. ) ;
#142076=PLANE ( 'NONE',  #138543 ) ;
#142077=AXIS2_PLACEMENT_3D ( 'NONE', #88048, #75060, #85899 ) ;
#142078=CARTESIAN_POINT ( 'NONE',  ( -32.20710678118632586, -20.24070752338406720, 5.000000000000000000 ) ) ;
#142080=EDGE_CURVE ( 'NONE', #68374, #35947, #47718, .T. ) ;
#142081=EDGE_LOOP ( 'NONE', ( #134728, #65275, #2379, #55089 ) ) ;
#142082=ORIENTED_EDGE ( 'NONE', *, *, #67098, .F. ) ;
#142083=LINE ( 'NONE', #652, #33356 ) ;
#142084=VERTEX_POINT ( 'NONE', #25190 ) ;
#142085=EDGE_CURVE ( 'NONE', #132991, #7168, #12882, .T. ) ;
#142088=LINE ( 'NONE', #17415, #9694 ) ;
#142089=CARTESIAN_POINT ( 'NONE',  ( -32.99999999999976552, -12.03360074219761522, 5.000000000000000000 ) ) ;
#142090=LINE ( 'NONE', #75389, #90284 ) ;
#142091=ORIENTED_EDGE ( 'NONE', *, *, #122211, .F. ) ;
#142092=DIRECTION ( 'NONE',  ( -0.000000000000000000, -0.3543493200069152693, 0.9351131265310292928 ) ) ;
#142093=ORIENTED_EDGE ( 'NONE', *, *, #63682, .T. ) ;
#142094=VECTOR ( 'NONE', #137403, 1000.000000000000000 ) ;
#142096=VECTOR ( 'NONE', #76835, 1000.000000000000227 ) ;
#142098=ORIENTED_EDGE ( 'NONE', *, *, #65335, .T. ) ;
#142102=EDGE_CURVE ( 'NONE', #120930, #123203, #23029, .T. ) ;
#142103=CARTESIAN_POINT ( 'NONE',  ( -29.99999999999978328, -16.02097659208072855, -11.96015758381201444 ) ) ;
#142104=VERTEX_POINT ( 'NONE', #123830 ) ;
#142105=ORIENTED_EDGE ( 'NONE', *, *, #31375, .F. ) ;
#142107=EDGE_LOOP ( 'NONE', ( #44819, #117513, #109082, #3625 ) ) ;
#142108=LINE ( 'NONE', #20280, #85625 ) ;
#142109=VECTOR ( 'NONE', #67020, 1000.000000000000000 ) ;
#142110=DIRECTION ( 'NONE',  ( 0.7071067811865487940, 0.7071067811865463515, 0.000000000000000000 ) ) ;
#142111=DIRECTION ( 'NONE',  ( 0.7071067811865487940, 0.7071067811865463515, -0.000000000000000000 ) ) ;
#142112=CARTESIAN_POINT ( 'NONE',  ( -30.48921356237309510, -27.52281430457076894, 5.000000000000000000 ) ) ;
#142113=ORIENTED_EDGE ( 'NONE', *, *, #49438, .T. ) ;
#142114=CARTESIAN_POINT ( 'NONE',  ( 34.92499999999998295, 18.20450307870172324, 3.476483422452878447 ) ) ;
#142115=LINE ( 'NONE', #18124, #90618 ) ;
#142116=CARTESIAN_POINT ( 'NONE',  ( -29.99451991528749417, 28.92564299267958816, 4.000000000000000000 ) ) ;
#142117=VERTEX_POINT ( 'NONE', #68053 ) ;
#142118=DIRECTION ( 'NONE',  ( -0.6830127018922180770, -0.6830127018922204085, -0.2588190451025213501 ) ) ;
#142119=AXIS2_PLACEMENT_3D ( 'NONE', #50268, #126377, #106027 ) ;
#142120=CARTESIAN_POINT ( 'NONE',  ( -36.18398860626899705, 28.73617430169812437, 5.000000000000000000 ) ) ;
#142121=VERTEX_POINT ( 'NONE', #101335 ) ;
#142123=VERTEX_POINT ( 'NONE', #123111 ) ;
#142125=VERTEX_POINT ( 'NONE', #34667 ) ;
#142127=LINE ( 'NONE', #85560, #26181 ) ;
#142128=LINE ( 'NONE', #85562, #87738 ) ;
#142129=VERTEX_POINT ( 'NONE', #1971 ) ;
#142130=LINE ( 'NONE', #129075, #125269 ) ;
#142131=CARTESIAN_POINT ( 'NONE',  ( -17.99999999999987210, -21.03360074219752462, 5.000000000000000000 ) ) ;
#142134=VECTOR ( 'NONE', #16141, 999.9999999999998863 ) ;
#142136=LINE ( 'NONE', #130540, #23475 ) ;
#142137=CARTESIAN_POINT ( 'NONE',  ( 27.79289321881326558, 0.7592924766157104211, 5.000000000000000000 ) ) ;
#142139=LINE ( 'NONE', #53698, #87655 ) ;
#142140=PLANE ( 'NONE',  #92060 ) ;
#142141=LINE ( 'NONE', #97904, #65250 ) ;
#142142=PLANE ( 'NONE',  #134009 ) ;
#142143=DIRECTION ( 'NONE',  ( -0.7071067811865487940, 0.7071067811865463515, 0.000000000000000000 ) ) ;
#142145=ORIENTED_EDGE ( 'NONE', *, *, #30398, .T. ) ;
#142146=AXIS2_PLACEMENT_3D ( 'NONE', #125265, #59332, #25954 ) ;
#142147=EDGE_CURVE ( 'NONE', #81437, #21537, #57869, .T. ) ;
#142148=ORIENTED_EDGE ( 'NONE', *, *, #19160, .F. ) ;
#142151=EDGE_CURVE ( 'NONE', #22356, #6977, #67300, .T. ) ;
#142152=ORIENTED_EDGE ( 'NONE', *, *, #39946, .F. ) ;
#142153=ORIENTED_EDGE ( 'NONE', *, *, #134682, .F. ) ;
#142154=ORIENTED_EDGE ( 'NONE', *, *, #79847, .T. ) ;
#142156=PLANE ( 'NONE',  #4563 ) ;
#142157=ORIENTED_EDGE ( 'NONE', *, *, #10569, .F. ) ;
#142159=FACE_OUTER_BOUND ( 'NONE', #18089, .T. ) ;
#142160=CARTESIAN_POINT ( 'NONE',  ( -23.99999999999983302, -16.06887692260764666, 4.000000000000000000 ) ) ;
#142161=LINE ( 'NONE', #19638, #37293 ) ;
#142162=ORIENTED_EDGE ( 'NONE', *, *, #954, .F. ) ;
#142163=EDGE_CURVE ( 'NONE', #68937, #16896, #35410, .T. ) ;
#142164=LINE ( 'NONE', #64580, #92792 ) ;
#142166=CIRCLE ( 'NONE', #7894, 5.968999999999998529 ) ;
#142167=CARTESIAN_POINT ( 'NONE',  ( 23.99451991528749062, 28.92564299267954908, 4.000000000000000000 ) ) ;
#142169=LINE ( 'NONE', #19645, #47737 ) ;
#142172=VECTOR ( 'NONE', #82776, 1000.000000000000000 ) ;
#142173=VERTEX_POINT ( 'NONE', #33960 ) ;
#142174=ORIENTED_EDGE ( 'NONE', *, *, #21725, .T. ) ;
#142177=DIRECTION ( 'NONE',  ( -0.6830127018922181881, 0.6830127018922202975, -0.2588190451025214056 ) ) ;
#142179=CARTESIAN_POINT ( 'NONE',  ( -29.67183060077626422, -3.740707523384238176, 4.000000000000000000 ) ) ;
#142181=DIRECTION ( 'NONE',  ( 0.7071067811865487940, 0.7071067811865463515, 0.000000000000000000 ) ) ;
#142182=LINE ( 'NONE', #89905, #113830 ) ;
#142183=CARTESIAN_POINT ( 'NONE',  ( -15.48921356237309510, -27.52281430457066236, 5.000000000000000000 ) ) ;
#142185=VECTOR ( 'NONE', #141553, 1000.000000000000000 ) ;
#142186=EDGE_LOOP ( 'NONE', ( #21045, #122469, #45610, #98056 ) ) ;
#142187=EDGE_CURVE ( 'NONE', #121941, #111265, #133966, .T. ) ;
#142188=VERTEX_POINT ( 'NONE', #2728 ) ;
#142189=CARTESIAN_POINT ( 'NONE',  ( 33.70710678118631165, -3.740707523384253719, 5.000000000000000000 ) ) ;
#142191=AXIS2_PLACEMENT_3D ( 'NONE', #123408, #34964, #3013 ) ;
#142192=LINE ( 'NONE', #8059, #30294 ) ;
#142193=ORIENTED_EDGE ( 'NONE', *, *, #82591, .F. ) ;
#142195=AXIS2_PLACEMENT_3D ( 'NONE', #833, #13133, #132106 ) ;
#142197=DIRECTION ( 'NONE',  ( -0.6830127018922180770, 0.6830127018922202975, -0.2588190451025213501 ) ) ;
#142198=FACE_OUTER_BOUND ( 'NONE', #134205, .T. ) ;
#142199=CARTESIAN_POINT ( 'NONE',  ( 27.18398860626900060, 28.73617430169806042, 5.000000000000000000 ) ) ;
#142200=PLANE ( 'NONE',  #108566 ) ;
#142201=AXIS2_PLACEMENT_3D ( 'NONE', #15075, #25247, #59348 ) ;
#142202=EDGE_CURVE ( 'NONE', #5968, #40900, #19913, .T. ) ;
#142204=EDGE_CURVE ( 'NONE', #1190, #130461, #36104, .T. ) ;
#142205=ORIENTED_EDGE ( 'NONE', *, *, #72172, .T. ) ;
#142206=CARTESIAN_POINT ( 'NONE',  ( 7.171830600776424092, -14.24070752338414003, 4.000000000000000000 ) ) ;
#142207=EDGE_CURVE ( 'NONE', #134120, #126282, #131291, .T. ) ;
#142209=ORIENTED_EDGE ( 'NONE', *, *, #60574, .T. ) ;
#142210=ORIENTED_EDGE ( 'NONE', *, *, #84284, .T. ) ;
#142211=EDGE_CURVE ( 'NONE', #131756, #121582, #131582, .T. ) ;
#142212=CARTESIAN_POINT ( 'NONE',  ( -54.48921356237310221, -27.52281430457093236, 5.000000000000000000 ) ) ;
#142214=ORIENTED_EDGE ( 'NONE', *, *, #54220, .T. ) ;
#142215=FACE_OUTER_BOUND ( 'NONE', #143411, .T. ) ;
#142216=ADVANCED_FACE ( 'NONE', ( #18678 ), #100388, .F. ) ;
#142217=LINE ( 'NONE', #66081, #10766 ) ;
#142218=VECTOR ( 'NONE', #83630, 999.9999999999998863 ) ;
#142220=DIRECTION ( 'NONE',  ( 0.3543493200069162685, -0.000000000000000000, -0.9351131265310288487 ) ) ;
#142221=ADVANCED_FACE ( 'NONE', ( #1032 ), #21393, .F. ) ;
#142222=FACE_BOUND ( 'NONE', #72288, .T. ) ;
#142223=ORIENTED_EDGE ( 'NONE', *, *, #112601, .F. ) ;
#142224=ADVANCED_FACE ( 'NONE', ( #132322 ), #89493, .T. ) ;
#142225=FACE_OUTER_BOUND ( 'NONE', #47051, .T. ) ;
#142226=FACE_OUTER_BOUND ( 'NONE', #17600, .T. ) ;
#142227=LINE ( 'NONE', #9510, #9131 ) ;
#142228=VERTEX_POINT ( 'NONE', #67043 ) ;
#142229=CARTESIAN_POINT ( 'NONE',  ( -1.499999999999984013, 0.05218569542916363935, 5.000000000000000000 ) ) ;
#142230=VERTEX_POINT ( 'NONE', #133728 ) ;
#142231=EDGE_LOOP ( 'NONE', ( #21689, #74125, #27796, #119127 ) ) ;
#142232=FACE_OUTER_BOUND ( 'NONE', #16892, .T. ) ;
#142233=EDGE_CURVE ( 'NONE', #81784, #75896, #11918, .T. ) ;
#142236=ORIENTED_EDGE ( 'NONE', *, *, #81757, .T. ) ;
#142237=CARTESIAN_POINT ( 'NONE',  ( 45.48921356237309510, -27.52281430457087197, 5.000000000000000000 ) ) ;
#142238=ORIENTED_EDGE ( 'NONE', *, *, #83088, .T. ) ;
#142239=DIRECTION ( 'NONE',  ( 0.7071067811865487940, -0.7071067811865463515, 0.000000000000000000 ) ) ;
#142240=CARTESIAN_POINT ( 'NONE',  ( -11.51078643762690490, -27.52281430457047406, 5.000000000000000000 ) ) ;
#142241=ORIENTED_EDGE ( 'NONE', *, *, #67809, .T. ) ;
#142242=DIRECTION ( 'NONE',  ( -0.6830127018922180770, -0.6830127018922204085, -0.2588190451025213501 ) ) ;
#142243=LINE ( 'NONE', #126503, #62017 ) ;
#142244=VECTOR ( 'NONE', #43270, 999.9999999999998863 ) ;
#142245=DIRECTION ( 'NONE',  ( 0.7071067811865486830, -0.7071067811865464625, -0.000000000000000000 ) ) ;
#142247=CARTESIAN_POINT ( 'NONE',  ( 34.42499999999998295, -10.45860074219784330, 5.000000000000000000 ) ) ;
#142248=DIRECTION ( 'NONE',  ( 0.7071067811865487940, 0.7071067811865463515, -0.000000000000000000 ) ) ;
#142249=DIRECTION ( 'NONE',  ( -0.3543493200069162685, -0.000000000000000000, -0.9351131265310288487 ) ) ;
#142250=VERTEX_POINT ( 'NONE', #62955 ) ;
#142251=EDGE_CURVE ( 'NONE', #61103, #34098, #120672, .T. ) ;
#142254=DIRECTION ( 'NONE',  ( -0.3543493200069163240, 4.681814790819596721E-17, -0.9351131265310288487 ) ) ;
#142255=DIRECTION ( 'NONE',  ( -0.000000000000000000, -0.3543493200069152693, 0.9351131265310292928 ) ) ;
#142257=EDGE_LOOP ( 'NONE', ( #50490, #99660, #61940, #27641 ) ) ;
#142258=CARTESIAN_POINT ( 'NONE',  ( -33.48921356237309510, -27.52281430457078670, 5.000000000000000000 ) ) ;
#142259=LINE ( 'NONE', #99412, #22433 ) ;
#142260=PLANE ( 'NONE',  #115708 ) ;
#142261=VERTEX_POINT ( 'NONE', #142466 ) ;
#142262=PLANE ( 'NONE',  #32426 ) ;
#142263=VECTOR ( 'NONE', #96543, 1000.000000000000000 ) ;
#142264=CARTESIAN_POINT ( 'NONE',  ( -60.18398860626900415, 28.73617430169829490, 5.000000000000000000 ) ) ;
#142265=AXIS2_PLACEMENT_3D ( 'NONE', #60150, #38379, #68890 ) ;
#142267=CARTESIAN_POINT ( 'NONE',  ( -15.18398860626900237, 28.73617430169797871, 5.000000000000000000 ) ) ;
#142268=EDGE_LOOP ( 'NONE', ( #47948, #1171, #65413, #140933 ) ) ;
#142270=VECTOR ( 'NONE', #68363, 1000.000000000000000 ) ;
#142271=CARTESIAN_POINT ( 'NONE',  ( -11.70025512860841133, -27.71228299555198049, 4.000000000000000000 ) ) ;
#142272=EDGE_CURVE ( 'NONE', #88886, #103321, #73115, .T. ) ;
#142273=DIRECTION ( 'NONE',  ( -0.000000000000000000, -0.3543493200069152693, 0.9351131265310292928 ) ) ;
#142274=LINE ( 'NONE', #95, #5530 ) ;
#142275=ORIENTED_EDGE ( 'NONE', *, *, #95288, .F. ) ;
#142276=DIRECTION ( 'NONE',  ( -0.7071067811865487940, 0.7071067811865463515, -0.000000000000000000 ) ) ;
#142277=ORIENTED_EDGE ( 'NONE', *, *, #1478, .F. ) ;
#142279=FACE_OUTER_BOUND ( 'NONE', #59552, .T. ) ;
#142280=DIRECTION ( 'NONE',  ( -0.7071067811865487940, 0.7071067811865463515, -0.000000000000000000 ) ) ;
#142281=VERTEX_POINT ( 'NONE', #54747 ) ;
#142282=VECTOR ( 'NONE', #111407, 1000.000000000000000 ) ;
#142283=ADVANCED_FACE ( 'NONE', ( #11176 ), #17953, .F. ) ;
#142286=VERTEX_POINT ( 'NONE', #95543 ) ;
#142288=LINE ( 'NONE', #98055, #88635 ) ;
#142289=ORIENTED_EDGE ( 'NONE', *, *, #105646, .T. ) ;
#142290=CYLINDRICAL_SURFACE ( 'NONE', #80860, 0.5000000000000004441 ) ;
#142292=EDGE_CURVE ( 'NONE', #111382, #143133, #139804, .T. ) ;
#142293=EDGE_LOOP ( 'NONE', ( #13387, #68222, #94613, #23298 ) ) ;
#142294=FACE_OUTER_BOUND ( 'NONE', #66628, .T. ) ;
#142295=FACE_OUTER_BOUND ( 'NONE', #81583, .T. ) ;
#142296=ORIENTED_EDGE ( 'NONE', *, *, #43953, .F. ) ;
#142297=AXIS2_PLACEMENT_3D ( 'NONE', #4878, #84640, #95494 ) ;
#142300=VECTOR ( 'NONE', #113734, 1000.000000000000227 ) ;
#142302=DIRECTION ( 'NONE',  ( -0.7071067811865486830, -0.7071067811865464625, 0.000000000000000000 ) ) ;
#142306=FACE_OUTER_BOUND ( 'NONE', #111622, .T. ) ;
#142307=FACE_OUTER_BOUND ( 'NONE', #60495, .T. ) ;
#142308=CARTESIAN_POINT ( 'NONE',  ( 3.707106781186514599, 14.25929247661557575, 5.000000000000000000 ) ) ;
#142311=AXIS2_PLACEMENT_3D ( 'NONE', #133836, #35972, #123698 ) ;
#142312=ORIENTED_EDGE ( 'NONE', *, *, #50756, .T. ) ;
#142313=VERTEX_POINT ( 'NONE', #22080 ) ;
#142314=DIRECTION ( 'NONE',  ( 0.6830127018922180770, -0.6830127018922204085, -0.2588190451025213501 ) ) ;
#142315=EDGE_CURVE ( 'NONE', #103344, #41451, #33716, .T. ) ;
#142316=ORIENTED_EDGE ( 'NONE', *, *, #103664, .F. ) ;
#142317=ORIENTED_EDGE ( 'NONE', *, *, #101446, .T. ) ;
#142318=DIRECTION ( 'NONE',  ( -0.000000000000000000, 0.3543493200069153248, 0.9351131265310292928 ) ) ;
#142319=CARTESIAN_POINT ( 'NONE',  ( -72.29974487139158157, -27.71228299555256669, 4.000000000000000000 ) ) ;
#142320=VERTEX_POINT ( 'NONE', #84681 ) ;
#142321=DIRECTION ( 'NONE',  ( 0.6830127018922181881, 0.6830127018922202975, -0.2588190451025214056 ) ) ;
#142322=LINE ( 'NONE', #64033, #104566 ) ;
#142323=CARTESIAN_POINT ( 'NONE',  ( 34.92499999999998295, 22.22500000000000142, 4.000000000000000000 ) ) ;
#142324=EDGE_CURVE ( 'NONE', #50292, #131000, #76504, .T. ) ;
#142325=PLANE ( 'NONE',  #46546 ) ;
#142326=DIRECTION ( 'NONE',  ( 0.7071067811865487940, 0.7071067811865463515, 0.000000000000000000 ) ) ;
#142327=ORIENTED_EDGE ( 'NONE', *, *, #31824, .T. ) ;
#142328=EDGE_CURVE ( 'NONE', #5368, #127658, #29566, .T. ) ;
#142330=CARTESIAN_POINT ( 'NONE',  ( -21.32816939922338406, 20.25929247661551358, 4.000000000000000000 ) ) ;
#142331=DIRECTION ( 'NONE',  ( -0.7071067811865486830, -0.7071067811865464625, 0.000000000000000000 ) ) ;
#142332=CARTESIAN_POINT ( 'NONE',  ( -15.18398860626900237, 28.73617430169797871, 5.000000000000000000 ) ) ;
#142333=CARTESIAN_POINT ( 'NONE',  ( -48.18398860626899705, 28.73617430169820608, 5.000000000000000000 ) ) ;
#142335=DIRECTION ( 'NONE',  ( 0.7071067811865487940, 0.7071067811865463515, 0.000000000000000000 ) ) ;
#142336=VERTEX_POINT ( 'NONE', #33015 ) ;
#142337=ORIENTED_EDGE ( 'NONE', *, *, #27179, .F. ) ;
#142339=DIRECTION ( 'NONE',  ( -0.000000000000000000, 0.3543493200069153248, 0.9351131265310292928 ) ) ;
#142341=DIRECTION ( 'NONE',  ( -0.7071067811865486830, 0.7071067811865464625, 0.000000000000000000 ) ) ;
#142342=VERTEX_POINT ( 'NONE', #77231 ) ;
#142343=PLANE ( 'NONE',  #71095 ) ;
#142344=EDGE_CURVE ( 'NONE', #12589, #43910, #99642, .T. ) ;
#142345=AXIS2_PLACEMENT_3D ( 'NONE', #68102, #12934, #112976 ) ;
#142346=DIRECTION ( 'NONE',  ( -0.3543493200069162685, -0.000000000000000000, -0.9351131265310288487 ) ) ;
#142348=ORIENTED_EDGE ( 'NONE', *, *, #13438, .T. ) ;
#142349=LINE ( 'NONE', #122712, #75748 ) ;
#142350=ORIENTED_EDGE ( 'NONE', *, *, #41856, .T. ) ;
#142351=VERTEX_POINT ( 'NONE', #77922 ) ;
#142353=DIRECTION ( 'NONE',  ( 0.7071067811865487940, 0.7071067811865463515, -0.000000000000000000 ) ) ;
#142354=DIRECTION ( 'NONE',  ( -0.000000000000000000, -0.3543493200069152138, 0.9351131265310292928 ) ) ;
#142355=EDGE_LOOP ( 'NONE', ( #66905, #53707, #31951, #132785 ) ) ;
#142356=PLANE ( 'NONE',  #11747 ) ;
#142358=EDGE_LOOP ( 'NONE', ( #121675, #102860, #61571, #90704 ) ) ;
#142360=CARTESIAN_POINT ( 'NONE',  ( 4.828169399223499525, 21.75929247661549581, 4.000000000000000000 ) ) ;
#142361=LINE ( 'NONE', #107563, #54740 ) ;
#142363=DIRECTION ( 'NONE',  ( -0.000000000000000000, 0.000000000000000000, 1.000000000000000000 ) ) ;
#142364=VECTOR ( 'NONE', #25900, 1000.000000000000000 ) ;
#142365=ADVANCED_FACE ( 'NONE', ( #122110 ), #22765, .F. ) ;
#142366=VERTEX_POINT ( 'NONE', #39292 ) ;
#142367=LINE ( 'NONE', #43060, #26847 ) ;
#142369=EDGE_CURVE ( 'NONE', #43657, #41375, #38569, .T. ) ;
#142370=CIRCLE ( 'NONE', #8099, 5.968999999999998529 ) ;
#142371=PLANE ( 'NONE',  #71903 ) ;
#142372=CARTESIAN_POINT ( 'NONE',  ( 32.99999999999976552, -4.068876922607775448, 4.000000000000000000 ) ) ;
#142374=ORIENTED_EDGE ( 'NONE', *, *, #3479, .T. ) ;
#142376=FACE_OUTER_BOUND ( 'NONE', #140840, .T. ) ;
#142379=EDGE_CURVE ( 'NONE', #125764, #83371, #73356, .T. ) ;
#142380=EDGE_CURVE ( 'NONE', #100225, #43483, #82803, .T. ) ;
#142381=ORIENTED_EDGE ( 'NONE', *, *, #34263, .T. ) ;
#142382=VECTOR ( 'NONE', #126925, 1000.000000000000000 ) ;
#142383=CARTESIAN_POINT ( 'NONE',  ( 1.500000000000001332, -5.947814304570766986, 5.000000000000000000 ) ) ;
#142384=VERTEX_POINT ( 'NONE', #137895 ) ;
#142385=DIRECTION ( 'NONE',  ( -0.7071067811865487940, 0.7071067811865463515, -0.000000000000000000 ) ) ;
#142387=LINE ( 'NONE', #11830, #11848 ) ;
#142388=EDGE_CURVE ( 'NONE', #90074, #85291, #49483, .T. ) ;
#142389=FACE_BOUND ( 'NONE', #32513, .T. ) ;
#142390=EDGE_CURVE ( 'NONE', #137465, #97116, #61090, .T. ) ;
#142391=CARTESIAN_POINT ( 'NONE',  ( -36.18398860626899705, 28.73617430169812437, 5.000000000000000000 ) ) ;
#142392=LINE ( 'NONE', #109010, #108178 ) ;
#142393=CARTESIAN_POINT ( 'NONE',  ( -69.18398860626899705, 28.73617430169835529, 5.000000000000000000 ) ) ;
#142394=ORIENTED_EDGE ( 'NONE', *, *, #122530, .T. ) ;
#142395=DIRECTION ( 'NONE',  ( -0.000000000000000000, 0.3543493200069153248, 0.9351131265310292928 ) ) ;
#142397=EDGE_CURVE ( 'NONE', #48401, #127256, #84245, .T. ) ;
#142399=ORIENTED_EDGE ( 'NONE', *, *, #56835, .T. ) ;
#142400=VECTOR ( 'NONE', #56882, 999.9999999999998863 ) ;
#142401=VECTOR ( 'NONE', #132476, 1000.000000000000227 ) ;
#142402=EDGE_LOOP ( 'NONE', ( #93661, #118653, #102290, #120329 ) ) ;
#142404=VERTEX_POINT ( 'NONE', #72678 ) ;
#142406=CARTESIAN_POINT ( 'NONE',  ( -18.29974487139159223, -27.71228299555219010, 4.000000000000000000 ) ) ;
#142407=EDGE_LOOP ( 'NONE', ( #12994, #128048, #12970, #66292 ) ) ;
#142408=LINE ( 'NONE', #129356, #32825 ) ;
#142409=EDGE_CURVE ( 'NONE', #95511, #61485, #93670, .T. ) ;
#142410=LINE ( 'NONE', #62709, #68038 ) ;
#142411=FACE_OUTER_BOUND ( 'NONE', #38222, .T. ) ;
#142412=DIRECTION ( 'NONE',  ( 0.7071067811865487940, 0.7071067811865463515, -0.000000000000000000 ) ) ;
#142413=CARTESIAN_POINT ( 'NONE',  ( -20.99999999999984368, 8.816494571476647835, 4.604407763760409722 ) ) ;
#142414=LINE ( 'NONE', #119202, #97947 ) ;
#142415=PLANE ( 'NONE',  #113360 ) ;
#142416=ORIENTED_EDGE ( 'NONE', *, *, #17897, .T. ) ;
#142417=EDGE_CURVE ( 'NONE', #50406, #120761, #27674, .T. ) ;
#142418=CARTESIAN_POINT ( 'NONE',  ( -16.49999999999988276, 16.46639925780209168, 5.000000000000000000 ) ) ;
#142419=ORIENTED_EDGE ( 'NONE', *, *, #127720, .T. ) ;
#142420=PLANE ( 'NONE',  #12459 ) ;
#142422=ORIENTED_EDGE ( 'NONE', *, *, #16620, .T. ) ;
#142424=EDGE_CURVE ( 'NONE', #49858, #119902, #40718, .T. ) ;
#142426=EDGE_CURVE ( 'NONE', #30783, #49766, #67339, .T. ) ;
#142428=LINE ( 'NONE', #8981, #39028 ) ;
#142430=CARTESIAN_POINT ( 'NONE',  ( -14.39513766812470408, 21.75929247661548516, 21.32995629748189259 ) ) ;
#142433=VERTEX_POINT ( 'NONE', #52286 ) ;
#142434=ORIENTED_EDGE ( 'NONE', *, *, #50956, .T. ) ;
#142437=CARTESIAN_POINT ( 'NONE',  ( 34.42499999999998295, 17.97718569542920619, 5.000000000000000000 ) ) ;
#142438=ORIENTED_EDGE ( 'NONE', *, *, #59686, .F. ) ;
#142441=CARTESIAN_POINT ( 'NONE',  ( 9.489213562373095101, -27.52281430457062328, 5.000000000000000000 ) ) ;
#142442=DIRECTION ( 'NONE',  ( 0.7071067811865487940, -0.7071067811865463515, 0.000000000000000000 ) ) ;
#142443=ORIENTED_EDGE ( 'NONE', *, *, #43472, .F. ) ;
#142444=LINE ( 'NONE', #41687, #75923 ) ;
#142445=VERTEX_POINT ( 'NONE', #105933 ) ;
#142446=ORIENTED_EDGE ( 'NONE', *, *, #36805, .T. ) ;
#142447=ORIENTED_EDGE ( 'NONE', *, *, #115566, .F. ) ;
#142449=CARTESIAN_POINT ( 'NONE',  ( 10.31275183893061431, -22.22500000000000142, 22.14227524773687605 ) ) ;
#142450=DIRECTION ( 'NONE',  ( 1.000000000000000000, 0.000000000000000000, 0.000000000000000000 ) ) ;
#142451=LINE ( 'NONE', #64171, #138770 ) ;
#142452=DIRECTION ( 'NONE',  ( -0.7071067811865487940, 0.7071067811865463515, -0.000000000000000000 ) ) ;
#142453=DIRECTION ( 'NONE',  ( -0.6830127018922181881, 0.6830127018922202975, -0.2588190451025214056 ) ) ;
#142454=PLANE ( 'NONE',  #118871 ) ;
#142455=LINE ( 'NONE', #100376, #62226 ) ;
#142456=ORIENTED_EDGE ( 'NONE', *, *, #123823, .F. ) ;
#142457=EDGE_CURVE ( 'NONE', #108628, #107596, #94362, .T. ) ;
#142460=CARTESIAN_POINT ( 'NONE',  ( -34.45011844616454511, -19.48371918836232197, 5.000000000000000888 ) ) ;
#142461=VECTOR ( 'NONE', #19132, 1000.000000000000000 ) ;
#142462=DIRECTION ( 'NONE',  ( 0.7071067811865487940, 0.7071067811865463515, 0.000000000000000000 ) ) ;
#142463=VERTEX_POINT ( 'NONE', #63212 ) ;
#142464=DIRECTION ( 'NONE',  ( 0.7071067811865487940, 0.7071067811865463515, -0.000000000000000000 ) ) ;
#142465=( BOUNDED_CURVE ( )  B_SPLINE_CURVE ( 3, ( #102752, #46254, #90435, #22998 ),
 .UNSPECIFIED., .F., .T. ) 
 B_SPLINE_CURVE_WITH_KNOTS ( ( 4, 4 ),
 ( 5.920967161967927161, 7.341195215986644484 ),
 .UNSPECIFIED. ) 
 CURVE ( )  GEOMETRIC_REPRESENTATION_ITEM ( )  RATIONAL_B_SPLINE_CURVE ( ( 1.000000000000000000, 0.8388583629366599403, 0.8388583629366599403, 1.000000000000000000 ) ) 
 REPRESENTATION_ITEM ( '' )  );
#142466=CARTESIAN_POINT ( 'NONE',  ( -17.99999999999987210, -10.06887692260770883, 4.000000000000000000 ) ) ;
#142468=ORIENTED_EDGE ( 'NONE', *, *, #78922, .F. ) ;
#142470=ORIENTED_EDGE ( 'NONE', *, *, #123242, .F. ) ;
#142471=FACE_OUTER_BOUND ( 'NONE', #88300, .T. ) ;
#142472=CARTESIAN_POINT ( 'NONE',  ( -18.29974487139159223, -27.71228299555219010, 4.000000000000000000 ) ) ;
#142474=CARTESIAN_POINT ( 'NONE',  ( -34.92500000000001137, -21.28150956279555217, 4.759050581649342249 ) ) ;
#142476=CARTESIAN_POINT ( 'NONE',  ( 14.99451991528749595, 28.92564299267948513, 4.000000000000000000 ) ) ;
#142477=DIRECTION ( 'NONE',  ( -0.000000000000000000, -0.3543493200069152693, 0.9351131265310292928 ) ) ;
#142478=VECTOR ( 'NONE', #50113, 1000.000000000000227 ) ;
#142479=DIRECTION ( 'NONE',  ( -0.6830127018922180770, -0.6830127018922204085, -0.2588190451025213501 ) ) ;
#142480=DIRECTION ( 'NONE',  ( -0.7071067811865486830, -0.7071067811865464625, 0.000000000000000000 ) ) ;
#142481=EDGE_CURVE ( 'NONE', #112045, #132778, #40031, .T. ) ;
#142482=EDGE_LOOP ( 'NONE', ( #49069, #101660, #128205, #43224 ) ) ;
#142483=CARTESIAN_POINT ( 'NONE',  ( -74.99451991528749772, 28.92564299267990435, 4.000000000000000000 ) ) ;
#142484=VERTEX_POINT ( 'NONE', #133438 ) ;
#142485=DIRECTION ( 'NONE',  ( -0.7071067811865487940, 0.7071067811865463515, -0.000000000000000000 ) ) ;
#142486=DIRECTION ( 'NONE',  ( 0.7071067811865487940, -0.7071067811865463515, 0.000000000000000000 ) ) ;
#142487=EDGE_LOOP ( 'NONE', ( #90769, #122154, #68148, #124624 ) ) ;
#142488=DIRECTION ( 'NONE',  ( 0.6830127018922181881, 0.6830127018922202975, -0.2588190451025214056 ) ) ;
#142489=LINE ( 'NONE', #9809, #118207 ) ;
#142490=ORIENTED_EDGE ( 'NONE', *, *, #49916, .T. ) ;
#142493=DIRECTION ( 'NONE',  ( 0.7071067811865487940, 0.7071067811865463515, -0.000000000000000000 ) ) ;
#142495=ORIENTED_EDGE ( 'NONE', *, *, #107541, .T. ) ;
#142496=EDGE_CURVE ( 'NONE', #39702, #64814, #44298, .T. ) ;
#142498=DIRECTION ( 'NONE',  ( 0.3543493200069162685, -0.000000000000000000, -0.9351131265310288487 ) ) ;
#142499=DIRECTION ( 'NONE',  ( -0.000000000000000000, -0.3543493200069152693, 0.9351131265310292928 ) ) ;
#142501=AXIS2_PLACEMENT_3D ( 'NONE', #50678, #70344, #127522 ) ;
#142504=LINE ( 'NONE', #23559, #97205 ) ;
#142505=AXIS2_PLACEMENT_3D ( 'NONE', #88139, #18740, #11238 ) ;
#142506=CARTESIAN_POINT ( 'NONE',  ( 34.92499999999998295, -21.72500000000000142, 5.000000000000000000 ) ) ;
#142507=ORIENTED_EDGE ( 'NONE', *, *, #33873, .T. ) ;
#142509=AXIS2_PLACEMENT_3D ( 'NONE', #94277, #37786, #138513 ) ;
#142510=EDGE_CURVE ( 'NONE', #73074, #73177, #23200, .T. ) ;
#142512=LINE ( 'NONE', #8365, #39348 ) ;
#142514=VECTOR ( 'NONE', #5503, 1000.000000000000000 ) ;
#142515=ORIENTED_EDGE ( 'NONE', *, *, #105591, .T. ) ;
#142516=EDGE_CURVE ( 'NONE', #70885, #35824, #78337, .T. ) ;
#142518=EDGE_LOOP ( 'NONE', ( #143246, #19035, #579, #118541 ) ) ;
#142520=PLANE ( 'NONE',  #133435 ) ;
#142521=FACE_OUTER_BOUND ( 'NONE', #47665, .T. ) ;
#142523=EDGE_CURVE ( 'NONE', #14903, #71811, #119657, .T. ) ;
#142525=LINE ( 'NONE', #120740, #14172 ) ;
#142526=PLANE ( 'NONE',  #109009 ) ;
#142528=DIRECTION ( 'NONE',  ( -0.000000000000000000, 0.000000000000000000, 1.000000000000000000 ) ) ;
#142529=DIRECTION ( 'NONE',  ( 0.7071067811865486830, -0.7071067811865464625, -0.000000000000000000 ) ) ;
#142531=CARTESIAN_POINT ( 'NONE',  ( -3.792893218813427669, 0.7592924766157086447, 5.000000000000000000 ) ) ;
#142533=CARTESIAN_POINT ( 'NONE',  ( 48.48921356237309510, -27.52281430457089328, 5.000000000000000000 ) ) ;
#142534=DIRECTION ( 'NONE',  ( -0.7071067811865486830, 0.7071067811865464625, 0.000000000000000000 ) ) ;
#142535=ORIENTED_EDGE ( 'NONE', *, *, #22533, .T. ) ;
#142536=( BOUNDED_CURVE ( )  B_SPLINE_CURVE ( 3, ( #133736, #119952, #22772, #43872 ),
 .UNSPECIFIED., .F., .T. ) 
 B_SPLINE_CURVE_WITH_KNOTS ( ( 4, 4 ),
 ( 1.964434688349487423, 3.503810798801452187 ),
 .UNSPECIFIED. ) 
 CURVE ( )  GEOMETRIC_REPRESENTATION_ITEM ( )  RATIONAL_B_SPLINE_CURVE ( ( 1.000000000000000000, 0.8120851936182278408, 0.8120851936182278408, 1.000000000000000000 ) ) 
 REPRESENTATION_ITEM ( '' )  );
#142537=ORIENTED_EDGE ( 'NONE', *, *, #130042, .T. ) ;
#142539=ORIENTED_EDGE ( 'NONE', *, *, #86600, .F. ) ;
#142540=LINE ( 'NONE', #141079, #26751 ) ;
#142541=EDGE_CURVE ( 'NONE', #8157, #63249, #110218, .T. ) ;
#142542=FACE_OUTER_BOUND ( 'NONE', #65864, .T. ) ;
#142543=DIRECTION ( 'NONE',  ( -0.6830127018922180770, -0.6830127018922204085, -0.2588190451025213501 ) ) ;
#142544=DIRECTION ( 'NONE',  ( 0.7071067811865487940, 0.7071067811865463515, 0.000000000000000000 ) ) ;
#142545=ORIENTED_EDGE ( 'NONE', *, *, #75867, .T. ) ;
#142546=ORIENTED_EDGE ( 'NONE', *, *, #118336, .F. ) ;
#142547=LINE ( 'NONE', #65734, #7534 ) ;
#142549=EDGE_CURVE ( 'NONE', #39048, #38617, #34126, .T. ) ;
#142550=EDGE_CURVE ( 'NONE', #40586, #90219, #130593, .T. ) ;
#142551=ORIENTED_EDGE ( 'NONE', *, *, #105600, .F. ) ;
#142552=CARTESIAN_POINT ( 'NONE',  ( -18.53421140649331633, 9.121673282332597665, 4.000000000000000000 ) ) ;
#142553=DIRECTION ( 'NONE',  ( -0.7071067811865486830, -0.7071067811865464625, 0.000000000000000000 ) ) ;
#142554=LINE ( 'NONE', #110592, #39999 ) ;
#142555=EDGE_CURVE ( 'NONE', #86941, #69882, #25412, .T. ) ;
#142556=ORIENTED_EDGE ( 'NONE', *, *, #88062, .F. ) ;
#142557=ADVANCED_FACE ( 'NONE', ( #21083 ), #42158, .F. ) ;
#142558=FACE_BOUND ( 'NONE', #128294, .T. ) ;
#142561=FACE_OUTER_BOUND ( 'NONE', #9421, .T. ) ;
#142563=LINE ( 'NONE', #19343, #85882 ) ;
#142565=AXIS2_PLACEMENT_3D ( 'NONE', #125886, #128037, #38163 ) ;
#142567=ADVANCED_FACE ( 'NONE', ( #92755 ), #34844, .F. ) ;
#142570=VERTEX_POINT ( 'NONE', #123990 ) ;
#142571=ADVANCED_FACE ( 'NONE', ( #26099 ), #81940, .F. ) ;
#142572=AXIS2_PLACEMENT_3D ( 'NONE', #13951, #96312, #16638 ) ;
#142573=EDGE_LOOP ( 'NONE', ( #1025, #116310, #121911, #13207 ) ) ;
#142574=ADVANCED_FACE ( 'NONE', ( #123290 ), #23960, .F. ) ;
#142575=CARTESIAN_POINT ( 'NONE',  ( 0.000000000000000000, 0.000000000000000000, 5.000000000000000000 ) ) ;
#142576=LINE ( 'NONE', #43267, #30953 ) ;
#142577=EDGE_LOOP ( 'NONE', ( #142938, #89055, #51150, #71973 ) ) ;
#142579=DIRECTION ( 'NONE',  ( -0.7071067811865486830, -0.7071067811865464625, 0.000000000000000000 ) ) ;
#142580=CARTESIAN_POINT ( 'NONE',  ( -20.66652290003515446, 8.920938975803856863, 4.000000000000000000 ) ) ;
#142581=CARTESIAN_POINT ( 'NONE',  ( 9.707013264292969623, -21.74070752338406365, 4.999753212805217117 ) ) ;
#142582=EDGE_CURVE ( 'NONE', #62743, #43483, #68218, .T. ) ;
#142584=VERTEX_POINT ( 'NONE', #58781 ) ;
#142585=LINE ( 'NONE', #96878, #65811 ) ;
#142586=CARTESIAN_POINT ( 'NONE',  ( -9.299744871391588674, -27.71228299555212971, 4.000000000000000000 ) ) ;
#142587=VERTEX_POINT ( 'NONE', #36265 ) ;
#142589=EDGE_LOOP ( 'NONE', ( #40708, #129074, #95562, #119433 ) ) ;
#142592=VERTEX_POINT ( 'NONE', #124689 ) ;
#142593=AXIS2_PLACEMENT_3D ( 'NONE', #9848, #41058, #87433 ) ;
#142594=CARTESIAN_POINT ( 'NONE',  ( -13.49999999999989342, -11.94781430457069860, 5.000000000000000000 ) ) ;
#142596=CARTESIAN_POINT ( 'NONE',  ( 24.29974487139158867, -27.71228299555223273, 4.000000000000000000 ) ) ;
#142598=CARTESIAN_POINT ( 'NONE',  ( 6.489213562373093325, -27.52281430457059841, 5.000000000000000000 ) ) ;
#142599=VECTOR ( 'NONE', #62189, 1000.000000000000227 ) ;
#142601=ORIENTED_EDGE ( 'NONE', *, *, #131378, .T. ) ;
#142603=VECTOR ( 'NONE', #97142, 1000.000000000000000 ) ;
#142606=CARTESIAN_POINT ( 'NONE',  ( 1.499999999999994449, 4.466399257802216027, 5.000000000000000000 ) ) ;
#142607=DIRECTION ( 'NONE',  ( 0.7071067811865486830, -0.7071067811865464625, -0.000000000000000000 ) ) ;
#142608=ORIENTED_EDGE ( 'NONE', *, *, #88689, .T. ) ;
#142609=CARTESIAN_POINT ( 'NONE',  ( 19.05000000000000071, 3.174999999999997158, 0.000000000000000000 ) ) ;
#142610=ORIENTED_EDGE ( 'NONE', *, *, #90156, .T. ) ;
#142611=ORIENTED_EDGE ( 'NONE', *, *, #133847, .F. ) ;
#142612=EDGE_LOOP ( 'NONE', ( #69038, #128122, #120900, #9605 ) ) ;
#142614=VERTEX_POINT ( 'NONE', #89906 ) ;
#142615=LINE ( 'NONE', #131025, #67806 ) ;
#142616=LINE ( 'NONE', #66490, #118078 ) ;
#142618=CARTESIAN_POINT ( 'NONE',  ( 34.82816939922328459, 0.7592924766157034266, 4.000000000000000000 ) ) ;
#142619=ORIENTED_EDGE ( 'NONE', *, *, #7194, .F. ) ;
#142622=DIRECTION ( 'NONE',  ( 0.7071067811865487940, 0.7071067811865463515, 0.000000000000000000 ) ) ;
#142624=ORIENTED_EDGE ( 'NONE', *, *, #52401, .T. ) ;
#142625=EDGE_LOOP ( 'NONE', ( #137203, #9874, #14318, #119275 ) ) ;
#142626=ORIENTED_EDGE ( 'NONE', *, *, #73936, .T. ) ;
#142628=DIRECTION ( 'NONE',  ( 0.7071067811865487940, 0.7071067811865463515, -0.000000000000000000 ) ) ;
#142629=VECTOR ( 'NONE', #114995, 1000.000000000000000 ) ;
#142630=CARTESIAN_POINT ( 'NONE',  ( -21.48921356237309155, -27.52281430457070499, 5.000000000000000000 ) ) ;
#142631=CARTESIAN_POINT ( 'NONE',  ( 74.99451991528749772, 28.92564299267990435, 4.000000000000000000 ) ) ;
#142634=CARTESIAN_POINT ( 'NONE',  ( 6.489213562373093325, -27.52281430457059841, 5.000000000000000000 ) ) ;
#142635=PLANE ( 'NONE',  #23386 ) ;
#142637=DIRECTION ( 'NONE',  ( -0.7071067811865486830, 0.7071067811865464625, 0.000000000000000000 ) ) ;
#142638=ORIENTED_EDGE ( 'NONE', *, *, #103835, .F. ) ;
#142641=EDGE_CURVE ( 'NONE', #50766, #22876, #13754, .T. ) ;
#142642=PLANE ( 'NONE',  #143218 ) ;
#142644=ORIENTED_EDGE ( 'NONE', *, *, #120169, .F. ) ;
#142645=EDGE_CURVE ( 'NONE', #117995, #119169, #35583, .T. ) ;
#142646=CARTESIAN_POINT ( 'NONE',  ( -71.99451991528749772, 28.92564299267988304, 4.000000000000000000 ) ) ;
#142648=DIRECTION ( 'NONE',  ( 0.6830127018922180770, -0.6830127018922204085, -0.2588190451025213501 ) ) ;
#142649=EDGE_LOOP ( 'NONE', ( #88297, #75510, #97525, #7705 ) ) ;
#142650=CARTESIAN_POINT ( 'NONE',  ( -19.05000000000000071, 3.174999999999997158, 4.000000000000000000 ) ) ;
#142652=EDGE_CURVE ( 'NONE', #35109, #30178, #103622, .T. ) ;
#142653=ADVANCED_FACE ( 'NONE', ( #4261 ), #1450, .F. ) ;
#142654=VECTOR ( 'NONE', #71436, 1000.000000000000000 ) ;
#142656=PLANE ( 'NONE',  #97086 ) ;
#142657=CARTESIAN_POINT ( 'NONE',  ( -14.67183060077636370, 20.25929247661551358, 4.000000000000000000 ) ) ;
#142658=VECTOR ( 'NONE', #114365, 1000.000000000000000 ) ;
#142659=ADVANCED_FACE ( 'NONE', ( #24653 ), #79812, .F. ) ;
#142660=DIRECTION ( 'NONE',  ( -0.000000000000000000, -0.3543493200069152693, 0.9351131265310292928 ) ) ;
#142661=DIRECTION ( 'NONE',  ( -0.000000000000000000, 0.000000000000000000, 1.000000000000000000 ) ) ;
#142662=CARTESIAN_POINT ( 'NONE',  ( 3.489213562373097322, -27.52281430457057709, 5.000000000000000000 ) ) ;
#142665=LINE ( 'NONE', #119450, #51325 ) ;
#142666=LINE ( 'NONE', #121605, #142699 ) ;
#142667=ORIENTED_EDGE ( 'NONE', *, *, #85392, .F. ) ;
#142668=ORIENTED_EDGE ( 'NONE', *, *, #58339, .F. ) ;
#142669=EDGE_CURVE ( 'NONE', #123192, #27739, #135585, .T. ) ;
#142670=CARTESIAN_POINT ( 'NONE',  ( -12.18398860626900060, 28.73617430169795739, 5.000000000000000000 ) ) ;
#142671=ORIENTED_EDGE ( 'NONE', *, *, #2735, .F. ) ;
#142672=AXIS2_PLACEMENT_3D ( 'NONE', #114532, #138446, #58799 ) ;
#142673=DIRECTION ( 'NONE',  ( 0.6830127018922181881, 0.6830127018922202975, -0.2588190451025214056 ) ) ;
#142674=CARTESIAN_POINT ( 'NONE',  ( 37.60343192894620756, -14.24070752338413293, 19.24067776001734487 ) ) ;
#142675=DIRECTION ( 'NONE',  ( 0.7071067811865487940, 0.7071067811865463515, -0.000000000000000000 ) ) ;
#142676=ORIENTED_EDGE ( 'NONE', *, *, #86194, .F. ) ;
#142678=DIRECTION ( 'NONE',  ( -0.7071067811865486830, -0.7071067811865464625, 0.000000000000000000 ) ) ;
#142679=FACE_OUTER_BOUND ( 'NONE', #142862, .T. ) ;
#142680=LINE ( 'NONE', #43372, #99816 ) ;
#142681=VECTOR ( 'NONE', #15185, 1000.000000000000000 ) ;
#142682=LINE ( 'NONE', #12156, #107663 ) ;
#142683=ORIENTED_EDGE ( 'NONE', *, *, #25832, .F. ) ;
#142684=CARTESIAN_POINT ( 'NONE',  ( 39.48921356237310221, -27.52281430457082934, 5.000000000000000000 ) ) ;
#142685=EDGE_CURVE ( 'NONE', #133116, #34514, #18754, .T. ) ;
#142687=CARTESIAN_POINT ( 'NONE',  ( 21.48921356237309155, -27.52281430457070499, 5.000000000000000000 ) ) ;
#142688=VECTOR ( 'NONE', #26288, 1000.000000000000000 ) ;
#142689=CARTESIAN_POINT ( 'NONE',  ( 34.47516574401890921, -7.509482387884292898, 4.998110765256834398 ) ) ;
#142690=AXIS2_PLACEMENT_3D ( 'NONE', #44509, #88711, #132943 ) ;
#142691=ORIENTED_EDGE ( 'NONE', *, *, #127861, .F. ) ;
#142692=EDGE_LOOP ( 'NONE', ( #119840, #88208, #35621, #18553 ) ) ;
#142693=ORIENTED_EDGE ( 'NONE', *, *, #95459, .F. ) ;
#142696=ORIENTED_EDGE ( 'NONE', *, *, #71896, .T. ) ;
#142697=ADVANCED_FACE ( 'NONE', ( #117348 ), #52118, .T. ) ;
#142699=VECTOR ( 'NONE', #31067, 1000.000000000000000 ) ;
#142700=DIRECTION ( 'NONE',  ( -0.7071067811865486830, -0.7071067811865464625, 0.000000000000000000 ) ) ;
#142701=EDGE_LOOP ( 'NONE', ( #106315, #128073, #68766, #72916 ) ) ;
#142703=LINE ( 'NONE', #42701, #67458 ) ;
#142704=ADVANCED_FACE ( 'NONE', ( #105069 ), #39850, .F. ) ;
#142705=EDGE_CURVE ( 'NONE', #28732, #55970, #27491, .T. ) ;
#142708=CARTESIAN_POINT ( 'NONE',  ( -34.17183060077622514, 12.75929247661558641, 4.000000000000000000 ) ) ;
#142709=CARTESIAN_POINT ( 'NONE',  ( -12.70710678118645554, -0.7407075233842718154, 5.000000000000000000 ) ) ;
#142710=EDGE_CURVE ( 'NONE', #139710, #66308, #140546, .T. ) ;
#142711=EDGE_LOOP ( 'NONE', ( #24246, #107229, #81228 ) ) ;
#142712=ORIENTED_EDGE ( 'NONE', *, *, #110667, .F. ) ;
#142713=ORIENTED_EDGE ( 'NONE', *, *, #65306, .F. ) ;
#142714=LINE ( 'NONE', #10047, #125593 ) ;
#142715=ADVANCED_FACE ( 'NONE', ( #61605 ), #116659, .F. ) ;
#142716=CARTESIAN_POINT ( 'NONE',  ( -22.95484226663318950, -21.74070752338405299, 21.72585301388579282 ) ) ;
#142720=CARTESIAN_POINT ( 'NONE',  ( -15.48921356237309510, -27.52281430457066236, 5.000000000000000000 ) ) ;
#142722=ORIENTED_EDGE ( 'NONE', *, *, #70092, .T. ) ;
#142723=ORIENTED_EDGE ( 'NONE', *, *, #26273, .F. ) ;
#142724=EDGE_CURVE ( 'NONE', #86087, #52679, #71044, .T. ) ;
#142725=LINE ( 'NONE', #55020, #50285 ) ;
#142727=ORIENTED_EDGE ( 'NONE', *, *, #128203, .F. ) ;
#142731=PLANE ( 'NONE',  #86820 ) ;
#142732=ORIENTED_EDGE ( 'NONE', *, *, #53845, .F. ) ;
#142734=LINE ( 'NONE', #85474, #111017 ) ;
#142735=DIRECTION ( 'NONE',  ( -0.000000000000000000, 0.3543493200069153248, 0.9351131265310292928 ) ) ;
#142736=VECTOR ( 'NONE', #37643, 999.9999999999998863 ) ;
#142737=DIRECTION ( 'NONE',  ( -0.7071067811865486830, -0.7071067811865464625, 0.000000000000000000 ) ) ;
#142738=( BOUNDED_CURVE ( )  B_SPLINE_CURVE ( 3, ( #98281, #76542, #7672, #75818 ),
 .UNSPECIFIED., .F., .T. ) 
 B_SPLINE_CURVE_WITH_KNOTS ( ( 4, 4 ),
 ( 2.779374508378133601, 4.199602562396796301 ),
 .UNSPECIFIED. ) 
 CURVE ( )  GEOMETRIC_REPRESENTATION_ITEM ( )  RATIONAL_B_SPLINE_CURVE ( ( 1.000000000000000000, 0.8388583629366717087, 0.8388583629366717087, 1.000000000000000000 ) ) 
 REPRESENTATION_ITEM ( '' )  );
#142739=CARTESIAN_POINT ( 'NONE',  ( -39.29974487139159578, -27.71228299555233576, 4.000000000000000000 ) ) ;
#142740=EDGE_LOOP ( 'NONE', ( #11632, #47633, #20655 ) ) ;
#142741=CARTESIAN_POINT ( 'NONE',  ( -23.99451991528749062, 28.92564299267954908, 4.000000000000000000 ) ) ;
#142742=ORIENTED_EDGE ( 'NONE', *, *, #143059, .T. ) ;
#142743=PLANE ( 'NONE',  #101280 ) ;
#142744=VERTEX_POINT ( 'NONE', #83334 ) ;
#142745=LINE ( 'NONE', #137411, #23846 ) ;
#142746=VERTEX_POINT ( 'NONE', #127539 ) ;
#142747=DIRECTION ( 'NONE',  ( -0.6830127018922181881, 0.6830127018922202975, -0.2588190451025214056 ) ) ;
#142748=ORIENTED_EDGE ( 'NONE', *, *, #42904, .T. ) ;
#142749=EDGE_LOOP ( 'NONE', ( #96613, #48965, #90908, #92261 ) ) ;
#142750=ORIENTED_EDGE ( 'NONE', *, *, #77386, .F. ) ;
#142751=AXIS2_PLACEMENT_3D ( 'NONE', #86431, #40781, #97244 ) ;
#142752=DIRECTION ( 'NONE',  ( -1.000000000000000000, 0.000000000000000000, 0.000000000000000000 ) ) ;
#142753=PLANE ( 'NONE',  #100793 ) ;
#142754=CARTESIAN_POINT ( 'NONE',  ( 60.18398860626900415, 28.73617430169829490, 5.000000000000000000 ) ) ;
#142755=CARTESIAN_POINT ( 'NONE',  ( 33.29974487139158867, -27.71228299555229313, 4.000000000000000000 ) ) ;
#142756=VECTOR ( 'NONE', #16268, 999.9999999999998863 ) ;
#142758=DIRECTION ( 'NONE',  ( -0.6830127018922181881, 0.6830127018922202975, -0.2588190451025214056 ) ) ;
#142760=LINE ( 'NONE', #34014, #85273 ) ;
#142762=CARTESIAN_POINT ( 'NONE',  ( -13.49999999999990408, -4.533600742197688938, 5.000000000000000000 ) ) ;
#142763=CARTESIAN_POINT ( 'NONE',  ( -34.92500000000001137, -14.66188269655941490, 18.97781875781096872 ) ) ;
#142764=CARTESIAN_POINT ( 'NONE',  ( -6.489213562373093325, -27.52281430457059841, 5.000000000000000000 ) ) ;
#142766=EDGE_LOOP ( 'NONE', ( #65574, #52376, #23236, #70229 ) ) ;
#142767=ORIENTED_EDGE ( 'NONE', *, *, #91339, .F. ) ;
#142768=VERTEX_POINT ( 'NONE', #49998 ) ;
#142769=CARTESIAN_POINT ( 'NONE',  ( 30.32816939922331656, -12.74070752338415247, 4.000000000000000000 ) ) ;
#142771=VERTEX_POINT ( 'NONE', #93489 ) ;
#142772=LINE ( 'NONE', #133342, #141665 ) ;
#142774=LINE ( 'NONE', #121013, #98825 ) ;
#142775=VECTOR ( 'NONE', #143239, 1000.000000000000000 ) ;
#142776=CARTESIAN_POINT ( 'NONE',  ( -13.49999999999991473, 8.319652575858375698, -8.582050562765859425 ) ) ;
#142777=ORIENTED_EDGE ( 'NONE', *, *, #16648, .T. ) ;
#142778=CARTESIAN_POINT ( 'NONE',  ( 1.040834085586084257E-14, 17.96639925780208102, 5.000000000000000000 ) ) ;
#142783=CARTESIAN_POINT ( 'NONE',  ( -50.99451991528749062, 28.92564299267973738, 4.000000000000000000 ) ) ;
#142784=VECTOR ( 'NONE', #91177, 1000.000000000000000 ) ;
#142786=ORIENTED_EDGE ( 'NONE', *, *, #65268, .F. ) ;
#142788=DIRECTION ( 'NONE',  ( 0.7071067811865486830, -0.7071067811865464625, -0.000000000000000000 ) ) ;
#142789=FACE_OUTER_BOUND ( 'NONE', #140133, .T. ) ;
#142791=ORIENTED_EDGE ( 'NONE', *, *, #15123, .F. ) ;
#142793=ORIENTED_EDGE ( 'NONE', *, *, #19814, .F. ) ;
#142794=ORIENTED_EDGE ( 'NONE', *, *, #54914, .F. ) ;
#142796=AXIS2_PLACEMENT_3D ( 'NONE', #55669, #130374, #110018 ) ;
#142797=LINE ( 'NONE', #97870, #116825 ) ;
#142798=LINE ( 'NONE', #7251, #123668 ) ;
#142799=ORIENTED_EDGE ( 'NONE', *, *, #15469, .T. ) ;
#142803=CARTESIAN_POINT ( 'NONE',  ( 5.125146193092313673, -14.24070752338413293, 9.401115078912647860 ) ) ;
#142804=EDGE_CURVE ( 'NONE', #131546, #25358, #7880, .T. ) ;
#142805=EDGE_LOOP ( 'NONE', ( #119726, #117203, #6889, #2814 ) ) ;
#142806=DIRECTION ( 'NONE',  ( 0.3543493200069162685, -0.000000000000000000, -0.9351131265310288487 ) ) ;
#142807=DIRECTION ( 'NONE',  ( 0.6830127018922181881, 0.6830127018922202975, -0.2588190451025214056 ) ) ;
#142808=ORIENTED_EDGE ( 'NONE', *, *, #98334, .T. ) ;
#142809=EDGE_CURVE ( 'NONE', #68414, #126070, #137723, .T. ) ;
#142810=CARTESIAN_POINT ( 'NONE',  ( -21.18398860626899349, 28.73617430169802134, 5.000000000000000000 ) ) ;
#142811=ORIENTED_EDGE ( 'NONE', *, *, #70857, .F. ) ;
#142812=VERTEX_POINT ( 'NONE', #38398 ) ;
#142813=ADVANCED_FACE ( 'NONE', ( #16622 ), #128269, .F. ) ;
#142814=ADVANCED_FACE ( 'NONE', ( #39108 ), #28234, .T. ) ;
#142815=DIRECTION ( 'NONE',  ( 0.6830127018922180770, -0.6830127018922204085, -0.2588190451025213501 ) ) ;
#142816=DIRECTION ( 'NONE',  ( -0.7071067811865486830, 0.7071067811865464625, 0.000000000000000000 ) ) ;
#142818=EDGE_LOOP ( 'NONE', ( #104034, #128589, #22274, #136682 ) ) ;
#142819=PLANE ( 'NONE',  #18876 ) ;
#142820=ADVANCED_FACE ( 'NONE', ( #106460 ), #126806, .F. ) ;
#142821=EDGE_CURVE ( 'NONE', #7821, #65237, #76760, .T. ) ;
#142822=LINE ( 'NONE', #87013, #107678 ) ;
#142823=VECTOR ( 'NONE', #67770, 1000.000000000000000 ) ;
#142825=PLANE ( 'NONE',  #27611 ) ;
#142829=DIRECTION ( 'NONE',  ( -0.7071067811865486830, 0.7071067811865464625, 0.000000000000000000 ) ) ;
#142830=DIRECTION ( 'NONE',  ( 0.7071067811865487940, 0.7071067811865463515, 0.000000000000000000 ) ) ;
#142831=FACE_OUTER_BOUND ( 'NONE', #18187, .T. ) ;
#142832=CARTESIAN_POINT ( 'NONE',  ( -19.49999999999986500, -11.94781430457070748, 5.000000000000000000 ) ) ;
#142834=CARTESIAN_POINT ( 'NONE',  ( 35.99451991528749772, 28.92564299267963079, 4.000000000000000000 ) ) ;
#142835=EDGE_CURVE ( 'NONE', #10226, #70306, #142703, .T. ) ;
#142836=PLANE ( 'NONE',  #111321 ) ;
#142837=DIRECTION ( 'NONE',  ( -0.3543493200069162685, -0.000000000000000000, -0.9351131265310288487 ) ) ;
#142838=ORIENTED_EDGE ( 'NONE', *, *, #52520, .T. ) ;
#142839=ORIENTED_EDGE ( 'NONE', *, *, #6036, .F. ) ;
#142842=VERTEX_POINT ( 'NONE', #87606 ) ;
#142843=EDGE_LOOP ( 'NONE', ( #90921, #106001, #120350, #61970 ) ) ;
#142844=VERTEX_POINT ( 'NONE', #21642 ) ;
#142845=VECTOR ( 'NONE', #18914, 1000.000000000000000 ) ;
#142846=CARTESIAN_POINT ( 'NONE',  ( -60.48921356237309510, -27.52281430457097500, 5.000000000000000000 ) ) ;
#142847=DIRECTION ( 'NONE',  ( 0.7071067811865487940, -0.7071067811865463515, 0.000000000000000000 ) ) ;
#142848=VERTEX_POINT ( 'NONE', #120937 ) ;
#142849=CARTESIAN_POINT ( 'NONE',  ( -65.99451991528749772, 28.92564299267984396, 4.000000000000000000 ) ) ;
#142850=CARTESIAN_POINT ( 'NONE',  ( -13.77325839282158348, -11.24070752338416845, 18.24660765846979515 ) ) ;
#142852=CARTESIAN_POINT ( 'NONE',  ( -3.299744871391591339, -27.71228299555208352, 4.000000000000000000 ) ) ;
#142853=VERTEX_POINT ( 'NONE', #76016 ) ;
#142855=DIRECTION ( 'NONE',  ( 1.000000000000000000, 0.000000000000000000, 0.000000000000000000 ) ) ;
#142856=EDGE_CURVE ( 'NONE', #2559, #98151, #130414, .T. ) ;
#142857=CARTESIAN_POINT ( 'NONE',  ( -11.81601139373100651, 28.73617430169779041, 5.000000000000000000 ) ) ;
#142861=CARTESIAN_POINT ( 'NONE',  ( -44.99451991528749772, 28.92564299267969474, 4.000000000000000000 ) ) ;
#142862=EDGE_LOOP ( 'NONE', ( #70769, #77645, #116293, #116237 ) ) ;
#142863=ORIENTED_EDGE ( 'NONE', *, *, #108622, .F. ) ;
#142866=ORIENTED_EDGE ( 'NONE', *, *, #36337, .T. ) ;
#142867=CARTESIAN_POINT ( 'NONE',  ( -26.18753812416034421, -22.22500000000000142, 4.000000000000000000 ) ) ;
#142869=CARTESIAN_POINT ( 'NONE',  ( 24.48921356237309510, -27.52281430457072631, 5.000000000000000000 ) ) ;
#142870=CARTESIAN_POINT ( 'NONE',  ( -34.82816939922328459, -17.24070752338410628, 4.000000000000000000 ) ) ;
#142871=DIRECTION ( 'NONE',  ( 0.7071067811865486830, -0.7071067811865464625, -0.000000000000000000 ) ) ;
#142873=EDGE_CURVE ( 'NONE', #50863, #81209, #43396, .T. ) ;
#142875=ORIENTED_EDGE ( 'NONE', *, *, #129670, .T. ) ;
#142876=EDGE_CURVE ( 'NONE', #136035, #62317, #108600, .T. ) ;
#142877=ORIENTED_EDGE ( 'NONE', *, *, #61142, .F. ) ;
#142879=DIRECTION ( 'NONE',  ( -0.7071067811865486830, -0.7071067811865464625, -0.000000000000000000 ) ) ;
#142880=EDGE_CURVE ( 'NONE', #13716, #56693, #11435, .T. ) ;
#142882=VERTEX_POINT ( 'NONE', #9280 ) ;
#142885=VERTEX_POINT ( 'NONE', #141258 ) ;
#142886=LINE ( 'NONE', #63913, #137386 ) ;
#142888=DIRECTION ( 'NONE',  ( -0.7071067811865486830, -0.7071067811865464625, 0.000000000000000000 ) ) ;
#142889=EDGE_CURVE ( 'NONE', #118345, #26318, #30364, .T. ) ;
#142890=VECTOR ( 'NONE', #87736, 999.9999999999998863 ) ;
#142894=ORIENTED_EDGE ( 'NONE', *, *, #132764, .F. ) ;
#142896=LINE ( 'NONE', #66769, #75736 ) ;
#142897=ORIENTED_EDGE ( 'NONE', *, *, #38638, .F. ) ;
#142898=EDGE_LOOP ( 'NONE', ( #28621, #47296, #36960 ) ) ;
#142899=VECTOR ( 'NONE', #40883, 1000.000000000000000 ) ;
#142901=DIRECTION ( 'NONE',  ( -0.7071067811865486830, -0.7071067811865464625, 0.000000000000000000 ) ) ;
#142902=ORIENTED_EDGE ( 'NONE', *, *, #45682, .F. ) ;
#142904=CARTESIAN_POINT ( 'NONE',  ( 72.48921356237309510, -27.52281430457106026, 5.000000000000000000 ) ) ;
#142905=FACE_OUTER_BOUND ( 'NONE', #79577, .T. ) ;
#142906=PLANE ( 'NONE',  #32706 ) ;
#142908=FACE_BOUND ( 'NONE', #4341, .T. ) ;
#142909=ORIENTED_EDGE ( 'NONE', *, *, #104244, .T. ) ;
#142910=CARTESIAN_POINT ( 'NONE',  ( -54.18398860626899705, 28.73617430169825226, 5.000000000000000000 ) ) ;
#142911=DIRECTION ( 'NONE',  ( -0.6830127018922180770, -0.6830127018922204085, -0.2588190451025213501 ) ) ;
#142912=LINE ( 'NONE', #43597, #2210 ) ;
#142913=ORIENTED_EDGE ( 'NONE', *, *, #70324, .T. ) ;
#142914=DIRECTION ( 'NONE',  ( 0.6830127018922180770, -0.6830127018922204085, -0.2588190451025213501 ) ) ;
#142915=VERTEX_POINT ( 'NONE', #22311 ) ;
#142916=VECTOR ( 'NONE', #51858, 1000.000000000000227 ) ;
#142918=DIRECTION ( 'NONE',  ( -0.3543493200069162685, -0.000000000000000000, -0.9351131265310288487 ) ) ;
#142919=( BOUNDED_CURVE ( )  B_SPLINE_CURVE ( 3, ( #84627, #128828, #61481, #136855 ),
 .UNSPECIFIED., .F., .T. ) 
 B_SPLINE_CURVE_WITH_KNOTS ( ( 4, 4 ),
 ( 1.864375635226908301, 1.933014472006540752 ),
 .UNSPECIFIED. ) 
 CURVE ( )  GEOMETRIC_REPRESENTATION_ITEM ( )  RATIONAL_B_SPLINE_CURVE ( ( 1.000000000000000000, 0.9996074310407762065, 0.9996074310407762065, 1.000000000000000000 ) ) 
 REPRESENTATION_ITEM ( '' )  );
#142920=VERTEX_POINT ( 'NONE', #66582 ) ;
#142923=ORIENTED_EDGE ( 'NONE', *, *, #38896, .F. ) ;
#142924=CARTESIAN_POINT ( 'NONE',  ( -39.29974487139159578, -27.71228299555233576, 4.000000000000000000 ) ) ;
#142925=CARTESIAN_POINT ( 'NONE',  ( 18.29974487139159223, -27.71228299555219010, 4.000000000000000000 ) ) ;
#142926=DIRECTION ( 'NONE',  ( -1.000000000000000000, 0.000000000000000000, 0.000000000000000000 ) ) ;
#142927=EDGE_LOOP ( 'NONE', ( #46648, #81840, #33714, #89826 ) ) ;
#142928=LINE ( 'NONE', #98698, #86203 ) ;
#142930=VECTOR ( 'NONE', #93310, 1000.000000000000000 ) ;
#142931=EDGE_CURVE ( 'NONE', #102772, #85411, #19488, .T. ) ;
#142932=ADVANCED_FACE ( 'NONE', ( #52808 ), #97005, .F. ) ;
#142933=DIRECTION ( 'NONE',  ( -0.6830127018922180770, -0.6830127018922204085, -0.2588190451025213501 ) ) ;
#142934=DIRECTION ( 'NONE',  ( -0.000000000000000000, -0.3543493200069152693, 0.9351131265310292928 ) ) ;
#142935=CARTESIAN_POINT ( 'NONE',  ( -8.510786437626906675, -27.52281430457049183, 5.000000000000000000 ) ) ;
#142936=LINE ( 'NONE', #132082, #4653 ) ;
#142938=ORIENTED_EDGE ( 'NONE', *, *, #123722, .T. ) ;
#142939=VERTEX_POINT ( 'NONE', #89057 ) ;
#142940=CARTESIAN_POINT ( 'NONE',  ( 18.48921356237309510, -27.52281430457068367, 5.000000000000000000 ) ) ;
#142941=CARTESIAN_POINT ( 'NONE',  ( -29.99451991528749417, 28.92564299267958816, 4.000000000000000000 ) ) ;
#142942=ORIENTED_EDGE ( 'NONE', *, *, #127215, .F. ) ;
#142943=ORIENTED_EDGE ( 'NONE', *, *, #128187, .T. ) ;
#142944=DIRECTION ( 'NONE',  ( -0.000000000000000000, 0.000000000000000000, 1.000000000000000000 ) ) ;
#142945=EDGE_CURVE ( 'NONE', #22423, #40143, #12881, .T. ) ;
#142946=CARTESIAN_POINT ( 'NONE',  ( 62.99451991528749772, 28.92564299267982264, 4.000000000000000000 ) ) ;
#142947=ORIENTED_EDGE ( 'NONE', *, *, #118928, .F. ) ;
#142948=CARTESIAN_POINT ( 'NONE',  ( -20.99999999999985789, 18.08204922493371214, 0.9627537363045357566 ) ) ;
#142949=CARTESIAN_POINT ( 'NONE',  ( -21.48921356237309155, -27.52281430457070499, 5.000000000000000000 ) ) ;
#142951=DIRECTION ( 'NONE',  ( 0.6830127018922180770, -0.6830127018922204085, -0.2588190451025213501 ) ) ;
#142952=ORIENTED_EDGE ( 'NONE', *, *, #2178, .F. ) ;
#142955=DIRECTION ( 'NONE',  ( -0.7071067811865486830, -0.7071067811865464625, 0.000000000000000000 ) ) ;
#142956=CARTESIAN_POINT ( 'NONE',  ( -16.43312800248732586, -21.74070752338406365, 6.915939825044111089 ) ) ;
#142957=PLANE ( 'NONE',  #139801 ) ;
#142958=ORIENTED_EDGE ( 'NONE', *, *, #11186, .T. ) ;
#142959=DIRECTION ( 'NONE',  ( -0.6830127018922180770, -0.6830127018922204085, -0.2588190451025213501 ) ) ;
#142960=VERTEX_POINT ( 'NONE', #122349 ) ;
#142962=PLANE ( 'NONE',  #132640 ) ;
#142963=CARTESIAN_POINT ( 'NONE',  ( 20.56494995367816614, -2.598550695876024275, 5.000000000000000000 ) ) ;
#142964=ORIENTED_EDGE ( 'NONE', *, *, #79105, .T. ) ;
#142965=AXIS2_PLACEMENT_3D ( 'NONE', #74944, #50318, #40863 ) ;
#142966=LINE ( 'NONE', #128540, #30264 ) ;
#142967=CARTESIAN_POINT ( 'NONE',  ( -34.47516574401891631, 21.02806734111560516, 4.998110765256836174 ) ) ;
#142968=ORIENTED_EDGE ( 'NONE', *, *, #119908, .T. ) ;
#142969=CARTESIAN_POINT ( 'NONE',  ( 13.17183060077638324, -5.240707523384225297, 4.000000000000000000 ) ) ;
#142972=EDGE_CURVE ( 'NONE', #102502, #100766, #101334, .T. ) ;
#142973=ORIENTED_EDGE ( 'NONE', *, *, #94322, .T. ) ;
#142976=FACE_OUTER_BOUND ( 'NONE', #108430, .T. ) ;
#142977=VERTEX_POINT ( 'NONE', #136102 ) ;
#142978=EDGE_CURVE ( 'NONE', #16368, #1674, #36103, .T. ) ;
#142979=ORIENTED_EDGE ( 'NONE', *, *, #76203, .T. ) ;
#142980=CARTESIAN_POINT ( 'NONE',  ( -9.888376381052353281, 9.759292476615614831, 17.35367589129214849 ) ) ;
#142982=AXIS2_PLACEMENT_3D ( 'NONE', #105113, #137765, #94933 ) ;
#142983=ORIENTED_EDGE ( 'NONE', *, *, #46571, .F. ) ;
#142984=AXIS2_PLACEMENT_3D ( 'NONE', #120405, #122575, #132791 ) ;
#142987=AXIS2_PLACEMENT_3D ( 'NONE', #10724, #9277, #143405 ) ;
#142988=ADVANCED_FACE ( 'NONE', ( #78174 ), #81032, .F. ) ;
#142990=CARTESIAN_POINT ( 'NONE',  ( -2.758305415748111944, 0.7592924766157069794, 14.37146558664983331 ) ) ;
#142991=EDGE_CURVE ( 'NONE', #7775, #64329, #36784, .T. ) ;
#142992=ORIENTED_EDGE ( 'NONE', *, *, #33053, .F. ) ;
#142993=CARTESIAN_POINT ( 'NONE',  ( -33.18398860626899705, 28.73617430169810305, 5.000000000000000000 ) ) ;
#142994=EDGE_CURVE ( 'NONE', #54350, #27936, #25921, .T. ) ;
#142995=PLANE ( 'NONE',  #102271 ) ;
#142996=DIRECTION ( 'NONE',  ( -0.000000000000000000, 0.3543493200069153248, 0.9351131265310292928 ) ) ;
#142997=VECTOR ( 'NONE', #37523, 1000.000000000000000 ) ;
#142999=EDGE_CURVE ( 'NONE', #8528, #69641, #91880, .T. ) ;
#143001=PLANE ( 'NONE',  #30304 ) ;
#143005=ADVANCED_FACE ( 'NONE', ( #134711 ), #70189, .F. ) ;
#143006=ORIENTED_EDGE ( 'NONE', *, *, #102272, .T. ) ;
#143007=ORIENTED_EDGE ( 'NONE', *, *, #91941, .F. ) ;
#143008=LINE ( 'NONE', #87908, #1545 ) ;
#143009=FACE_OUTER_BOUND ( 'NONE', #62306, .T. ) ;
#143010=EDGE_LOOP ( 'NONE', ( #79227, #55384, #26534, #112032 ) ) ;
#143012=CARTESIAN_POINT ( 'NONE',  ( 17.99451991528748351, 28.92564299267950645, 4.000000000000000000 ) ) ;
#143013=ADVANCED_FACE ( 'NONE', ( #68738 ), #23026, .F. ) ;
#143014=PLANE ( 'NONE',  #76509 ) ;
#143015=EDGE_CURVE ( 'NONE', #25993, #104365, #67299, .T. ) ;
#143016=DIRECTION ( 'NONE',  ( -0.7071067811865486830, -0.7071067811865464625, 0.000000000000000000 ) ) ;
#143018=EDGE_LOOP ( 'NONE', ( #25377, #136105, #123299, #87471 ) ) ;
#143021=AXIS2_PLACEMENT_3D ( 'NONE', #58107, #123345, #113135 ) ;
#143022=DIRECTION ( 'NONE',  ( -0.7071067811865487940, 0.7071067811865463515, -0.000000000000000000 ) ) ;
#143023=FACE_OUTER_BOUND ( 'NONE', #105480, .T. ) ;
#143024=DIRECTION ( 'NONE',  ( 0.7071067811865487940, 0.7071067811865463515, 0.000000000000000000 ) ) ;
#143025=EDGE_CURVE ( 'NONE', #142433, #91556, #102781, .T. ) ;
#143026=LINE ( 'NONE', #55318, #95432 ) ;
#143029=CARTESIAN_POINT ( 'NONE',  ( 20.99999999999983658, -16.02097659208071079, -11.96015758381214056 ) ) ;
#143031=CARTESIAN_POINT ( 'NONE',  ( -39.29974487139159578, -27.71228299555233576, 4.000000000000000000 ) ) ;
#143032=ORIENTED_EDGE ( 'NONE', *, *, #138710, .F. ) ;
#143033=EDGE_LOOP ( 'NONE', ( #63903, #82331, #93692, #133576 ) ) ;
#143035=CARTESIAN_POINT ( 'NONE',  ( 33.32816939922329169, 5.259292476615674339, 4.000000000000000000 ) ) ;
#143036=LINE ( 'NONE', #11056, #15975 ) ;
#143037=ORIENTED_EDGE ( 'NONE', *, *, #129091, .T. ) ;
#143038=CARTESIAN_POINT ( 'NONE',  ( -12.18398860626900060, 28.73617430169795739, 5.000000000000000000 ) ) ;
#143039=CARTESIAN_POINT ( 'NONE',  ( -2.277185695429367662, -21.72499999999999432, 5.000000000000000000 ) ) ;
#143042=EDGE_CURVE ( 'NONE', #10046, #143231, #103458, .T. ) ;
#143043=ORIENTED_EDGE ( 'NONE', *, *, #67931, .F. ) ;
#143044=ORIENTED_EDGE ( 'NONE', *, *, #16948, .T. ) ;
#143045=DIRECTION ( 'NONE',  ( -0.3543493200069162685, -0.000000000000000000, -0.9351131265310288487 ) ) ;
#143046=CARTESIAN_POINT ( 'NONE',  ( 18.24525979340076276, 9.091288135747575438, 4.682346157478786353 ) ) ;
#143047=DIRECTION ( 'NONE',  ( -1.000000000000000000, 0.000000000000000000, 0.000000000000000000 ) ) ;
#143049=ORIENTED_EDGE ( 'NONE', *, *, #67272, .F. ) ;
#143050=CARTESIAN_POINT ( 'NONE',  ( 63.48921356237309510, -27.52281430457099631, 5.000000000000000000 ) ) ;
#143052=ORIENTED_EDGE ( 'NONE', *, *, #60920, .F. ) ;
#143056=LINE ( 'NONE', #32158, #53852 ) ;
#143057=LINE ( 'NONE', #87256, #41648 ) ;
#143059=EDGE_CURVE ( 'NONE', #123911, #63022, #57161, .T. ) ;
#143060=ORIENTED_EDGE ( 'NONE', *, *, #68552, .T. ) ;
#143061=AXIS2_PLACEMENT_3D ( 'NONE', #102982, #50037, #3618 ) ;
#143065=EDGE_CURVE ( 'NONE', #20150, #34692, #133277, .T. ) ;
#143066=DIRECTION ( 'NONE',  ( -0.000000000000000000, 0.3543493200069153248, 0.9351131265310292928 ) ) ;
#143067=FACE_OUTER_BOUND ( 'NONE', #59531, .T. ) ;
#143068=ORIENTED_EDGE ( 'NONE', *, *, #66473, .F. ) ;
#143069=ORIENTED_EDGE ( 'NONE', *, *, #107656, .F. ) ;
#143071=DIRECTION ( 'NONE',  ( -0.6830127018922181881, 0.6830127018922202975, -0.2588190451025214056 ) ) ;
#143072=ORIENTED_EDGE ( 'NONE', *, *, #75932, .F. ) ;
#143073=ORIENTED_EDGE ( 'NONE', *, *, #141979, .F. ) ;
#143075=EDGE_CURVE ( 'NONE', #83238, #43157, #79650, .T. ) ;
#143076=CARTESIAN_POINT ( 'NONE',  ( -42.18398860626899705, 28.73617430169816700, 5.000000000000000000 ) ) ;
#143078=LINE ( 'NONE', #77831, #137175 ) ;
#143080=VECTOR ( 'NONE', #98904, 999.9999999999998863 ) ;
#143081=CARTESIAN_POINT ( 'NONE',  ( -11.99999999999993427, -22.22500000000000142, 4.412002311789994913 ) ) ;
#143082=AXIS2_PLACEMENT_3D ( 'NONE', #143088, #107595, #108273 ) ;
#143083=EDGE_CURVE ( 'NONE', #94901, #83408, #24486, .T. ) ;
#143084=FACE_BOUND ( 'NONE', #104160, .T. ) ;
#143085=CARTESIAN_POINT ( 'NONE',  ( 24.21271579574130683, 0.1791150535437372460, 5.000000000000000000 ) ) ;
#143086=DIRECTION ( 'NONE',  ( -0.7071067811865487940, 0.7071067811865463515, -0.000000000000000000 ) ) ;
#143087=DIRECTION ( 'NONE',  ( 0.7071067811865486830, -0.7071067811865464625, -0.000000000000000000 ) ) ;
#143088=CARTESIAN_POINT ( 'NONE',  ( 15.48921356237309510, -27.52281430457066236, 5.000000000000000000 ) ) ;
#143090=VECTOR ( 'NONE', #15919, 999.9999999999998863 ) ;
#143091=CARTESIAN_POINT ( 'NONE',  ( -6.792893218813405909, 18.75929247661552779, 5.000000000000000000 ) ) ;
#143092=ORIENTED_EDGE ( 'NONE', *, *, #109144, .T. ) ;
#143093=EDGE_CURVE ( 'NONE', #35075, #132490, #17186, .T. ) ;
#143094=VERTEX_POINT ( 'NONE', #138254 ) ;
#143096=VERTEX_POINT ( 'NONE', #95446 ) ;
#143097=DIRECTION ( 'NONE',  ( 0.7071067811865487940, 0.7071067811865463515, -0.000000000000000000 ) ) ;
#143098=CARTESIAN_POINT ( 'NONE',  ( 5.999999999999950262, -10.77435723561694836, -9.972017380717245416 ) ) ;
#143099=ORIENTED_EDGE ( 'NONE', *, *, #137597, .T. ) ;
#143100=LINE ( 'NONE', #55395, #118471 ) ;
#143101=ADVANCED_FACE ( 'NONE', ( #18573 ), #138977, .F. ) ;
#143102=LINE ( 'NONE', #7570, #17067 ) ;
#143103=DIRECTION ( 'NONE',  ( -0.7071067811865487940, 0.7071067811865463515, -0.000000000000000000 ) ) ;
#143104=EDGE_CURVE ( 'NONE', #137546, #86438, #82452, .T. ) ;
#143105=CARTESIAN_POINT ( 'NONE',  ( -5.816011393731002066, 28.73617430169783304, 5.000000000000000000 ) ) ;
#143106=FACE_OUTER_BOUND ( 'NONE', #58038, .T. ) ;
#143108=LINE ( 'NONE', #107614, #46983 ) ;
#143109=PLANE ( 'NONE',  #92551 ) ;
#143111=CARTESIAN_POINT ( 'NONE',  ( -36.48921356237310221, -27.52281430457080802, 5.000000000000000000 ) ) ;
#143112=VERTEX_POINT ( 'NONE', #15703 ) ;
#143114=VECTOR ( 'NONE', #119777, 1000.000000000000000 ) ;
#143115=ORIENTED_EDGE ( 'NONE', *, *, #84357, .F. ) ;
#143116=ORIENTED_EDGE ( 'NONE', *, *, #39651, .F. ) ;
#143118=PLANE ( 'NONE',  #25292 ) ;
#143119=AXIS2_PLACEMENT_3D ( 'NONE', #61320, #31325, #53804 ) ;
#143120=ORIENTED_EDGE ( 'NONE', *, *, #85186, .F. ) ;
#143121=CARTESIAN_POINT ( 'NONE',  ( -8.999999999999934275, -21.03360074219752462, 5.000000000000000000 ) ) ;
#143122=LINE ( 'NONE', #122067, #19192 ) ;
#143126=DIRECTION ( 'NONE',  ( 0.7071067811865487940, -0.7071067811865463515, 0.000000000000000000 ) ) ;
#143130=VECTOR ( 'NONE', #133329, 1000.000000000000227 ) ;
#143131=CARTESIAN_POINT ( 'NONE',  ( 34.45011844616453800, 18.00230414159375059, 5.000000000000001776 ) ) ;
#143132=VERTEX_POINT ( 'NONE', #94013 ) ;
#143133=VERTEX_POINT ( 'NONE', #73705 ) ;
#143134=PLANE ( 'NONE',  #132998 ) ;
#143135=( BOUNDED_CURVE ( )  B_SPLINE_CURVE ( 3, ( #100774, #46439, #56608, #122507 ),
 .UNSPECIFIED., .F., .F. ) 
 B_SPLINE_CURVE_WITH_KNOTS ( ( 4, 4 ),
 ( 1.975938068165229655, 2.025325302527092308 ),
 .UNSPECIFIED. ) 
 CURVE ( )  GEOMETRIC_REPRESENTATION_ITEM ( )  RATIONAL_B_SPLINE_CURVE ( ( 1.000000000000000000, 0.9997967520851089862, 0.9997967520851089862, 1.000000000000000000 ) ) 
 REPRESENTATION_ITEM ( '' )  );
#143136=CARTESIAN_POINT ( 'NONE',  ( 21.48921356237309155, -27.52281430457070499, 5.000000000000000000 ) ) ;
#143137=DIRECTION ( 'NONE',  ( 0.7071067811865487940, 0.7071067811865463515, 0.000000000000000000 ) ) ;
#143138=EDGE_LOOP ( 'NONE', ( #113098, #118934, #34656, #67760 ) ) ;
#143140=VERTEX_POINT ( 'NONE', #137548 ) ;
#143141=VERTEX_POINT ( 'NONE', #126636 ) ;
#143142=LINE ( 'NONE', #108332, #84283 ) ;
#143143=PLANE ( 'NONE',  #104231 ) ;
#143144=CARTESIAN_POINT ( 'NONE',  ( -20.99999999999985079, -10.44781430457071991, 5.000000000000000000 ) ) ;
#143145=DIRECTION ( 'NONE',  ( -0.3543493200069162685, -0.000000000000000000, -0.9351131265310288487 ) ) ;
#143146=LINE ( 'NONE', #1022, #90823 ) ;
#143147=DIRECTION ( 'NONE',  ( 0.3543493200069162685, -0.000000000000000000, -0.9351131265310288487 ) ) ;
#143148=DIRECTION ( 'NONE',  ( 0.7071067811865486830, -0.7071067811865464625, -0.000000000000000000 ) ) ;
#143149=ORIENTED_EDGE ( 'NONE', *, *, #72165, .T. ) ;
#143150=LINE ( 'NONE', #66328, #39683 ) ;
#143151=EDGE_LOOP ( 'NONE', ( #118124, #103051, #104724, #122377 ) ) ;
#143152=LINE ( 'NONE', #9779, #67926 ) ;
#143154=CARTESIAN_POINT ( 'NONE',  ( 42.48921356237308800, -27.52281430457085065, 5.000000000000000000 ) ) ;
#143155=EDGE_CURVE ( 'NONE', #10755, #107195, #136817, .T. ) ;
#143156=ORIENTED_EDGE ( 'NONE', *, *, #21128, .F. ) ;
#143157=CARTESIAN_POINT ( 'NONE',  ( -8.816011393731004731, 28.73617430169781173, 5.000000000000000000 ) ) ;
#143158=VECTOR ( 'NONE', #44552, 1000.000000000000000 ) ;
#143161=EDGE_LOOP ( 'NONE', ( #16768, #127081, #98693, #70741 ) ) ;
#143162=EDGE_CURVE ( 'NONE', #129256, #36084, #62130, .T. ) ;
#143163=ORIENTED_EDGE ( 'NONE', *, *, #35912, .T. ) ;
#143164=DIRECTION ( 'NONE',  ( -0.000000000000000000, 0.3543493200069153248, 0.9351131265310292928 ) ) ;
#143165=CARTESIAN_POINT ( 'NONE',  ( -54.18398860626899705, 28.73617430169825226, 5.000000000000000000 ) ) ;
#143166=EDGE_CURVE ( 'NONE', #108223, #59222, #107037, .T. ) ;
#143167=DIRECTION ( 'NONE',  ( 0.6830127018922180770, -0.6830127018922204085, -0.2588190451025213501 ) ) ;
#143168=LINE ( 'NONE', #319, #17346 ) ;
#143170=EDGE_CURVE ( 'NONE', #98588, #69496, #4824, .T. ) ;
#143173=DIRECTION ( 'NONE',  ( -0.7071067811865487940, 0.7071067811865463515, -0.000000000000000000 ) ) ;
#143174=DIRECTION ( 'NONE',  ( 0.6830127018922181881, 0.6830127018922202975, -0.2588190451025214056 ) ) ;
#143176=VERTEX_POINT ( 'NONE', #6965 ) ;
#143180=LINE ( 'NONE', #85948, #103161 ) ;
#143181=VECTOR ( 'NONE', #128822, 1000.000000000000000 ) ;
#143183=DIRECTION ( 'NONE',  ( -0.000000000000000000, 0.3543493200069153248, 0.9351131265310292928 ) ) ;
#143184=CARTESIAN_POINT ( 'NONE',  ( -66.48921356237309510, -27.52281430457101763, 5.000000000000000000 ) ) ;
#143186=ADVANCED_FACE ( 'NONE', ( #60736 ), #84596, .T. ) ;
#143187=CARTESIAN_POINT ( 'NONE',  ( -6.328169399223480873, 8.259292476615636147, 4.000000000000000000 ) ) ;
#143188=EDGE_CURVE ( 'NONE', #137381, #46584, #128106, .T. ) ;
#143189=CARTESIAN_POINT ( 'NONE',  ( 15.18398860626900237, 28.73617430169797871, 5.000000000000000000 ) ) ;
#143190=DIRECTION ( 'NONE',  ( 0.7071067811865487940, -0.7071067811865463515, 0.000000000000000000 ) ) ;
#143191=VERTEX_POINT ( 'NONE', #125958 ) ;
#143192=ORIENTED_EDGE ( 'NONE', *, *, #58748, .T. ) ;
#143194=AXIS2_PLACEMENT_3D ( 'NONE', #105135, #126867, #27554 ) ;
#143197=EDGE_CURVE ( 'NONE', #58012, #64733, #6253, .T. ) ;
#143198=CARTESIAN_POINT ( 'NONE',  ( -39.29974487139159578, -27.71228299555233576, 4.000000000000000000 ) ) ;
#143200=LINE ( 'NONE', #127705, #46370 ) ;
#143201=CARTESIAN_POINT ( 'NONE',  ( -7.499999999999947597, 19.39370406404967184, 1.459788787078221128 ) ) ;
#143202=ORIENTED_EDGE ( 'NONE', *, *, #57338, .T. ) ;
#143204=CARTESIAN_POINT ( 'NONE',  ( 0.000000000000000000, 0.000000000000000000, 5.000000000000000000 ) ) ;
#143205=LINE ( 'NONE', #107709, #53067 ) ;
#143206=PLANE ( 'NONE',  #68328 ) ;
#143208=ORIENTED_EDGE ( 'NONE', *, *, #72877, .F. ) ;
#143209=FACE_OUTER_BOUND ( 'NONE', #123560, .T. ) ;
#143210=ORIENTED_EDGE ( 'NONE', *, *, #101302, .T. ) ;
#143211=VECTOR ( 'NONE', #128912, 1000.000000000000000 ) ;
#143212=CARTESIAN_POINT ( 'NONE',  ( -31.49999999999978684, -17.56887692260763956, 4.000000000000000000 ) ) ;
#143214=LINE ( 'NONE', #87419, #119509 ) ;
#143215=EDGE_CURVE ( 'NONE', #105497, #89784, #72329, .T. ) ;
#143216=EDGE_LOOP ( 'NONE', ( #90239, #73320, #23102, #137494 ) ) ;
#143217=CARTESIAN_POINT ( 'NONE',  ( 51.48921356237309510, -27.52281430457091460, 5.000000000000000000 ) ) ;
#143218=AXIS2_PLACEMENT_3D ( 'NONE', #99102, #143344, #132520 ) ;
#143219=CARTESIAN_POINT ( 'NONE',  ( 7.499999999999951150, 16.46639925780209879, 5.000000000000000000 ) ) ;
#143220=DIRECTION ( 'NONE',  ( 0.7071067811865487940, 0.7071067811865463515, -0.000000000000000000 ) ) ;
#143221=VECTOR ( 'NONE', #47939, 1000.000000000000000 ) ;
#143222=CARTESIAN_POINT ( 'NONE',  ( 18.00548008471250583, 28.92564299267925776, 4.000000000000000000 ) ) ;
#143223=DIRECTION ( 'NONE',  ( -0.7071067811865486830, -0.7071067811865464625, -0.000000000000000000 ) ) ;
#143225=ORIENTED_EDGE ( 'NONE', *, *, #35943, .F. ) ;
#143226=DIRECTION ( 'NONE',  ( 0.7071067811865487940, 0.7071067811865463515, 0.000000000000000000 ) ) ;
#143227=CARTESIAN_POINT ( 'NONE',  ( 15.18398860626900237, 28.73617430169797871, 5.000000000000000000 ) ) ;
#143228=DIRECTION ( 'NONE',  ( -0.000000000000000000, 0.000000000000000000, 1.000000000000000000 ) ) ;
#143230=CARTESIAN_POINT ( 'NONE',  ( 28.82816939922332011, -14.24070752338414003, 4.000000000000000000 ) ) ;
#143231=VERTEX_POINT ( 'NONE', #116496 ) ;
#143232=EDGE_CURVE ( 'NONE', #122079, #861, #105590, .T. ) ;
#143233=ORIENTED_EDGE ( 'NONE', *, *, #29957, .F. ) ;
#143235=ORIENTED_EDGE ( 'NONE', *, *, #84301, .F. ) ;
#143236=CARTESIAN_POINT ( 'NONE',  ( 42.18398860626899705, 28.73617430169816700, 5.000000000000000000 ) ) ;
#143239=DIRECTION ( 'NONE',  ( -0.7071067811865486830, -0.7071067811865464625, -0.000000000000000000 ) ) ;
#143242=VECTOR ( 'NONE', #128020, 1000.000000000000000 ) ;
#143243=LINE ( 'NONE', #96840, #107091 ) ;
#143245=VECTOR ( 'NONE', #49606, 1000.000000000000000 ) ;
#143246=ORIENTED_EDGE ( 'NONE', *, *, #18258, .F. ) ;
#143247=EDGE_CURVE ( 'NONE', #21912, #5925, #73031, .T. ) ;
#143248=DIRECTION ( 'NONE',  ( -0.7071067811865486830, -0.7071067811865464625, 0.000000000000000000 ) ) ;
#143249=LINE ( 'NONE', #73710, #38587 ) ;
#143250=CARTESIAN_POINT ( 'NONE',  ( 12.48921356237309155, -27.52281430457064104, 5.000000000000000000 ) ) ;
#143252=ADVANCED_FACE ( 'NONE', ( #63581 ), #141084, .F. ) ;
#143253=FACE_BOUND ( 'NONE', #98810, .T. ) ;
#143254=DIRECTION ( 'NONE',  ( -0.7071067811865487940, 0.7071067811865463515, 0.000000000000000000 ) ) ;
#143255=DIRECTION ( 'NONE',  ( 0.7071067811865487940, 0.7071067811865463515, 0.000000000000000000 ) ) ;
#143256=DIRECTION ( 'NONE',  ( -0.6830127018922181881, 0.6830127018922202975, -0.2588190451025214056 ) ) ;
#143257=PLANE ( 'NONE',  #133679 ) ;
#143258=CARTESIAN_POINT ( 'NONE',  ( -20.27718569542926730, -21.72500000000000853, 5.000000000000000000 ) ) ;
#143260=ORIENTED_EDGE ( 'NONE', *, *, #130263, .F. ) ;
#143262=VERTEX_POINT ( 'NONE', #20014 ) ;
#143263=ORIENTED_EDGE ( 'NONE', *, *, #90587, .F. ) ;
#143264=LINE ( 'NONE', #34509, #79434 ) ;
#143265=LINE ( 'NONE', #77344, #77896 ) ;
#143266=DIRECTION ( 'NONE',  ( 0.6830127018922180770, -0.6830127018922202975, -0.2588190451025213501 ) ) ;
#143267=ORIENTED_EDGE ( 'NONE', *, *, #69450, .F. ) ;
#143269=LINE ( 'NONE', #118664, #142244 ) ;
#143270=EDGE_CURVE ( 'NONE', #138233, #74016, #33101, .T. ) ;
#143271=FACE_BOUND ( 'NONE', #127259, .T. ) ;
#143272=LINE ( 'NONE', #54863, #124498 ) ;
#143273=PLANE ( 'NONE',  #78183 ) ;
#143274=PLANE ( 'NONE',  #69312 ) ;
#143275=VECTOR ( 'NONE', #3631, 1000.000000000000000 ) ;
#143277=PLANE ( 'NONE',  #23568 ) ;
#143278=ORIENTED_EDGE ( 'NONE', *, *, #70092, .F. ) ;
#143279=LINE ( 'NONE', #76631, #82052 ) ;
#143280=PLANE ( 'NONE',  #25704 ) ;
#143281=VECTOR ( 'NONE', #142049, 1000.000000000000000 ) ;
#143283=EDGE_CURVE ( 'NONE', #66785, #99513, #88163, .T. ) ;
#143285=EDGE_CURVE ( 'NONE', #128234, #109338, #98327, .T. ) ;
#143286=EDGE_LOOP ( 'NONE', ( #35399, #3581, #117901, #42054, #39387, #140465 ) ) ;
#143287=EDGE_CURVE ( 'NONE', #99346, #118799, #64263, .T. ) ;
#143289=ORIENTED_EDGE ( 'NONE', *, *, #12154, .T. ) ;
#143290=VECTOR ( 'NONE', #92160, 1000.000000000000227 ) ;
#143291=DIRECTION ( 'NONE',  ( -0.000000000000000000, 0.3543493200069153248, 0.9351131265310292928 ) ) ;
#143295=CARTESIAN_POINT ( 'NONE',  ( 34.92499999999998295, -2.993876922608006641, 4.000000000000000000 ) ) ;
#143296=ORIENTED_EDGE ( 'NONE', *, *, #58353, .F. ) ;
#143297=FACE_OUTER_BOUND ( 'NONE', #7750, .T. ) ;
#143298=VECTOR ( 'NONE', #128383, 1000.000000000000000 ) ;
#143299=CARTESIAN_POINT ( 'NONE',  ( 25.01459476339044130, 2.945717840782780428, 4.000000000000000000 ) ) ;
#143301=CARTESIAN_POINT ( 'NONE',  ( 29.99999999999979394, 14.96639925780210056, 5.000000000000000000 ) ) ;
#143302=ORIENTED_EDGE ( 'NONE', *, *, #87534, .F. ) ;
#143303=AXIS2_PLACEMENT_3D ( 'NONE', #92530, #40349, #117844 ) ;
#143304=CARTESIAN_POINT ( 'NONE',  ( 34.75611968250419181, 1.705650698524030062, 4.955485411084880276 ) ) ;
#143305=EDGE_LOOP ( 'NONE', ( #59277, #62002, #20296, #24280 ) ) ;
#143306=ORIENTED_EDGE ( 'NONE', *, *, #80011, .T. ) ;
#143307=ORIENTED_EDGE ( 'NONE', *, *, #77214, .F. ) ;
#143310=VECTOR ( 'NONE', #11981, 1000.000000000000000 ) ;
#143311=AXIS2_PLACEMENT_3D ( 'NONE', #106064, #129263, #105373 ) ;
#143312=CARTESIAN_POINT ( 'NONE',  ( 9.328169399223463998, -15.74070752338411339, 4.000000000000000000 ) ) ;
#143313=VECTOR ( 'NONE', #21570, 1000.000000000000227 ) ;
#143314=DIRECTION ( 'NONE',  ( -0.3543493200069162685, -0.000000000000000000, -0.9351131265310288487 ) ) ;
#143315=VERTEX_POINT ( 'NONE', #108428 ) ;
#143316=CARTESIAN_POINT ( 'NONE',  ( 20.20666063542138247, 21.75929247661549581, 4.998822639870702744 ) ) ;
#143317=EDGE_LOOP ( 'NONE', ( #47960, #25598, #33414, #8722 ) ) ;
#143318=VECTOR ( 'NONE', #123058, 1000.000000000000000 ) ;
#143321=CARTESIAN_POINT ( 'NONE',  ( 4.171830600776441855, 0.7592924766157120864, 4.000000000000000000 ) ) ;
#143322=EDGE_CURVE ( 'NONE', #13795, #91413, #131667, .T. ) ;
#143323=CARTESIAN_POINT ( 'NONE',  ( -60.29974487139158867, -27.71228299555248142, 4.000000000000000000 ) ) ;
#143324=CARTESIAN_POINT ( 'NONE',  ( 34.49999999999976552, 3.054329344830917670, 4.994342998332163219 ) ) ;
#143325=ORIENTED_EDGE ( 'NONE', *, *, #23653, .F. ) ;
#143326=EDGE_CURVE ( 'NONE', #6884, #66617, #130246, .T. ) ;
#143327=VERTEX_POINT ( 'NONE', #120023 ) ;
#143328=EDGE_LOOP ( 'NONE', ( #108010, #123706, #37187, #81220 ) ) ;
#143331=AXIS2_PLACEMENT_3D ( 'NONE', #110322, #123403, #79195 ) ;
#143332=DIRECTION ( 'NONE',  ( -0.6830127018922180770, -0.6830127018922204085, -0.2588190451025213501 ) ) ;
#143333=CARTESIAN_POINT ( 'NONE',  ( 0.000000000000000000, 0.000000000000000000, 5.000000000000000000 ) ) ;
#143334=EDGE_CURVE ( 'NONE', #540, #124629, #43940, .T. ) ;
#143338=LINE ( 'NONE', #88984, #11935 ) ;
#143339=CARTESIAN_POINT ( 'NONE',  ( -11.33153258840135358, -18.74070752338409207, 20.73178291233838522 ) ) ;
#143340=EDGE_LOOP ( 'NONE', ( #92172, #52736, #112175, #47386 ) ) ;
#143341=DIRECTION ( 'NONE',  ( -0.6830127018922180770, -0.6830127018922204085, -0.2588190451025213501 ) ) ;
#143344=DIRECTION ( 'NONE',  ( 0.6830127018922180770, -0.6830127018922204085, -0.2588190451025213501 ) ) ;
#143345=DIRECTION ( 'NONE',  ( -0.6830127018922180770, -0.6830127018922204085, -0.2588190451025213501 ) ) ;
#143346=EDGE_LOOP ( 'NONE', ( #129862, #18718, #71623, #83898 ) ) ;
#143349=FACE_OUTER_BOUND ( 'NONE', #28465, .T. ) ;
#143350=ORIENTED_EDGE ( 'NONE', *, *, #78572, .F. ) ;
#143351=PLANE ( 'NONE',  #104045 ) ;
#143352=ORIENTED_EDGE ( 'NONE', *, *, #75926, .F. ) ;
#143353=DIRECTION ( 'NONE',  ( -0.7071067811865486830, -0.7071067811865464625, -0.000000000000000000 ) ) ;
#143355=ORIENTED_EDGE ( 'NONE', *, *, #72231, .F. ) ;
#143356=PLANE ( 'NONE',  #59199 ) ;
#143361=LINE ( 'NONE', #37482, #100188 ) ;
#143362=DIRECTION ( 'NONE',  ( -0.6830127018922181881, 0.6830127018922202975, -0.2588190451025214056 ) ) ;
#143363=LINE ( 'NONE', #9995, #117838 ) ;
#143367=CARTESIAN_POINT ( 'NONE',  ( 33.18398860626899705, 28.73617430169810305, 5.000000000000000000 ) ) ;
#143368=DIRECTION ( 'NONE',  ( -0.7071067811865486830, 0.7071067811865464625, 0.000000000000000000 ) ) ;
#143369=VERTEX_POINT ( 'NONE', #125052 ) ;
#143370=EDGE_LOOP ( 'NONE', ( #104804, #49515, #74225, #55671 ) ) ;
#143371=CARTESIAN_POINT ( 'NONE',  ( 31.49999999999977973, 19.39370406404970026, 1.459788787078129202 ) ) ;
#143372=VERTEX_POINT ( 'NONE', #80862 ) ;
#143374=CARTESIAN_POINT ( 'NONE',  ( -1.001930566820972812, -22.22500000000000142, 4.500000000000000888 ) ) ;
#143377=DIRECTION ( 'NONE',  ( -0.6830127018922181881, 0.6830127018922202975, -0.2588190451025214056 ) ) ;
#143379=VECTOR ( 'NONE', #17398, 1000.000000000000000 ) ;
#143380=VECTOR ( 'NONE', #61210, 1000.000000000000000 ) ;
#143382=DIRECTION ( 'NONE',  ( -0.6830127018922181881, 0.6830127018922202975, -0.2588190451025214056 ) ) ;
#143383=CARTESIAN_POINT ( 'NONE',  ( -8.721745484314221031, 8.259292476615634371, 11.78515199841148586 ) ) ;
#143389=ADVANCED_FACE ( 'NONE', ( #103988 ), #114177, .F. ) ;
#143390=ORIENTED_EDGE ( 'NONE', *, *, #2782, .F. ) ;
#143391=LINE ( 'NONE', #11413, #118668 ) ;
#143392=EDGE_CURVE ( 'NONE', #29382, #77043, #26464, .T. ) ;
#143394=LINE ( 'NONE', #44102, #89595 ) ;
#143395=AXIS2_PLACEMENT_3D ( 'NONE', #29590, #139831, #41925 ) ;
#143397=EDGE_CURVE ( 'NONE', #97559, #60588, #138811, .T. ) ;
#143399=ORIENTED_EDGE ( 'NONE', *, *, #16557, .T. ) ;
#143401=ORIENTED_EDGE ( 'NONE', *, *, #77283, .T. ) ;
#143402=CARTESIAN_POINT ( 'NONE',  ( 14.99999999999989875, -1.209798855135680418, 4.371887122346866050 ) ) ;
#143403=VECTOR ( 'NONE', #147, 1000.000000000000000 ) ;
#143404=CIRCLE ( 'NONE', #46167, 5.968999999999998529 ) ;
#143405=DIRECTION ( 'NONE',  ( 0.7071067811865487940, -0.7071067811865463515, 0.000000000000000000 ) ) ;
#143406=ORIENTED_EDGE ( 'NONE', *, *, #17465, .T. ) ;
#143407=CARTESIAN_POINT ( 'NONE',  ( -10.82816939922345867, 12.75929247661558641, 4.000000000000000000 ) ) ;
#143409=VECTOR ( 'NONE', #106077, 999.9999999999998863 ) ;
#143411=EDGE_LOOP ( 'NONE', ( #121542, #57367, #82561, #68679 ) ) ;
#143412=DIRECTION ( 'NONE',  ( 0.7071067811865486830, -0.7071067811865464625, -0.000000000000000000 ) ) ;
#143414=VECTOR ( 'NONE', #102437, 1000.000000000000000 ) ;
#143416=AXIS2_PLACEMENT_3D ( 'NONE', #84872, #129080, #61036 ) ;
#143419=ORIENTED_EDGE ( 'NONE', *, *, #63030, .T. ) ;
#143420=CARTESIAN_POINT ( 'NONE',  ( 0.000000000000000000, 0.000000000000000000, 5.000000000000000000 ) ) ;
#143422=DIRECTION ( 'NONE',  ( 1.000000000000000000, 0.000000000000000000, 0.000000000000000000 ) ) ;
#143423=VECTOR ( 'NONE', #113246, 1000.000000000000000 ) ;
#143424=CARTESIAN_POINT ( 'NONE',  ( 8.994519915287490619, 28.92564299267944250, 4.000000000000000000 ) ) ;
#143425=CARTESIAN_POINT ( 'NONE',  ( 6.328169399223488867, -6.740707523384212863, 4.000000000000000000 ) ) ;
#143426=ORIENTED_EDGE ( 'NONE', *, *, #139422, .T. ) ;
#143430=ORIENTED_EDGE ( 'NONE', *, *, #72407, .T. ) ;
#143431=VECTOR ( 'NONE', #79031, 1000.000000000000000 ) ;
#143432=DIRECTION ( 'NONE',  ( 0.3543493200069162685, -0.000000000000000000, -0.9351131265310288487 ) ) ;
#143436=LINE ( 'NONE', #109388, #68777 ) ;
#143437=DIRECTION ( 'NONE',  ( 0.7071067811865487940, 0.7071067811865463515, -0.000000000000000000 ) ) ;
#143439=ORIENTED_EDGE ( 'NONE', *, *, #127401, .T. ) ;
#143440=LINE ( 'NONE', #101369, #106599 ) ;
#143441=ORIENTED_EDGE ( 'NONE', *, *, #127423, .F. ) ;
#143444=VERTEX_POINT ( 'NONE', #17698 ) ;
#143445=CARTESIAN_POINT ( 'NONE',  ( -17.54016161050249423, 18.75929247661552779, 8.305906642995445566 ) ) ;
#143446=VERTEX_POINT ( 'NONE', #104728 ) ;
#143447=DIRECTION ( 'NONE',  ( -0.3543493200069163240, 0.000000000000000000, -0.9351131265310288487 ) ) ;
#143448=EDGE_CURVE ( 'NONE', #72122, #4103, #15538, .T. ) ;
#143449=ORIENTED_EDGE ( 'NONE', *, *, #82658, .F. ) ;
#143451=ORIENTED_EDGE ( 'NONE', *, *, #6383, .F. ) ;
#143453=CARTESIAN_POINT ( 'NONE',  ( 3.707106781186516375, -3.740707523384250166, 5.000000000000000000 ) ) ;
#143455=PLANE ( 'NONE',  #68132 ) ;
#143457=PLANE ( 'NONE',  #21861 ) ;
#143458=EDGE_CURVE ( 'NONE', #65352, #121929, #84440, .T. ) ;
#143459=DIRECTION ( 'NONE',  ( 1.000000000000000000, 0.000000000000000000, 0.000000000000000000 ) ) ;
#143461=CARTESIAN_POINT ( 'NONE',  ( -72.48921356237309510, -27.52281430457106026, 5.000000000000000000 ) ) ;
#143464=DIRECTION ( 'NONE',  ( 0.000000000000000000, 0.3543493200069153248, 0.9351131265310291818 ) ) ;
#143466=ORIENTED_EDGE ( 'NONE', *, *, #55911, .T. ) ;
#143467=ORIENTED_EDGE ( 'NONE', *, *, #116942, .T. ) ;
#143468=AXIS2_PLACEMENT_3D ( 'NONE', #34320, #78547, #122749 ) ;
#143469=ORIENTED_EDGE ( 'NONE', *, *, #2699, .T. ) ;
#143470=CARTESIAN_POINT ( 'NONE',  ( 35.99451991528749772, 28.92564299267963079, 4.000000000000000000 ) ) ;
#143471=VECTOR ( 'NONE', #15954, 1000.000000000000000 ) ;
#143472=EDGE_CURVE ( 'NONE', #9887, #141378, #138488, .T. ) ;
#143473=AXIS2_PLACEMENT_3D ( 'NONE', #96067, #34960, #79196 ) ;
#143474=EDGE_LOOP ( 'NONE', ( #102988, #30151, #8608, #21772 ) ) ;
#143475=AXIS2_PLACEMENT_3D ( 'NONE', #8139, #85010, #66143 ) ;
#143479=DIRECTION ( 'NONE',  ( 0.000000000000000000, -1.000000000000000000, 0.000000000000000000 ) ) ;
#143480=DIRECTION ( 'NONE',  ( 0.7071067811865487940, 0.7071067811865463515, -0.000000000000000000 ) ) ;
#143481=LINE ( 'NONE', #56538, #4648 ) ;
#143482=ORIENTED_EDGE ( 'NONE', *, *, #114676, .T. ) ;
#143483=LINE ( 'NONE', #66661, #71871 ) ;
#143484=EDGE_CURVE ( 'NONE', #119248, #11479, #93147, .T. ) ;
#143485=VECTOR ( 'NONE', #2487, 1000.000000000000000 ) ;
#143486=EDGE_LOOP ( 'NONE', ( #51238, #98368, #57675, #86786 ) ) ;
#143490=ORIENTED_EDGE ( 'NONE', *, *, #47699, .F. ) ;
#143493=FACE_OUTER_BOUND ( 'NONE', #85503, .T. ) ;
#143494=ORIENTED_EDGE ( 'NONE', *, *, #136352, .F. ) ;
#143495=ADVANCED_FACE ( 'NONE', ( #125790 ), #136635, .F. ) ;
#143496=EDGE_LOOP ( 'NONE', ( #42848, #78309, #121282, #20853 ) ) ;
#143497=ORIENTED_EDGE ( 'NONE', *, *, #1876, .T. ) ;
#143499=AXIS2_PLACEMENT_3D ( 'NONE', #56603, #2119, #80466 ) ;
#143500=FACE_OUTER_BOUND ( 'NONE', #38946, .T. ) ;
#143501=VECTOR ( 'NONE', #97735, 999.9999999999998863 ) ;
#143502=FACE_OUTER_BOUND ( 'NONE', #96418, .T. ) ;
#143503=DIRECTION ( 'NONE',  ( -0.7071067811865486830, 0.7071067811865464625, 0.000000000000000000 ) ) ;
#143504=LINE ( 'NONE', #88439, #109760 ) ;
#143505=ORIENTED_EDGE ( 'NONE', *, *, #68956, .F. ) ;
#143507=ADVANCED_FACE ( 'NONE', ( #82292 ), #98150, .F. ) ;
#143508=DIRECTION ( 'NONE',  ( -0.7071067811865487940, 0.7071067811865463515, -0.000000000000000000 ) ) ;
#143509=AXIS2_PLACEMENT_3D ( 'NONE', #116475, #95427, #83882 ) ;
#143512=EDGE_LOOP ( 'NONE', ( #7529, #12778, #105137, #87289 ) ) ;
#143513=DIRECTION ( 'NONE',  ( -0.7071067811865486830, -0.7071067811865464625, 0.000000000000000000 ) ) ;
#143515=CARTESIAN_POINT ( 'NONE',  ( 47.99451991528749062, 28.92564299267971251, 4.000000000000000000 ) ) ;
#143516=VECTOR ( 'NONE', #74763, 1000.000000000000000 ) ;
#143517=EDGE_CURVE ( 'NONE', #124853, #137018, #94012, .T. ) ;
#143518=VERTEX_POINT ( 'NONE', #74994 ) ;
#143519=LINE ( 'NONE', #97885, #48705 ) ;
#143520=EDGE_LOOP ( 'NONE', ( #54585, #137432, #123632, #49037 ) ) ;
#143521=EDGE_CURVE ( 'NONE', #37569, #46262, #131490, .T. ) ;
#143522=VERTEX_POINT ( 'NONE', #87270 ) ;
#143523=VECTOR ( 'NONE', #100630, 1000.000000000000000 ) ;
#143524=EDGE_CURVE ( 'NONE', #81752, #77753, #30014, .T. ) ;
#143525=FACE_OUTER_BOUND ( 'NONE', #20262, .T. ) ;
#143527=CARTESIAN_POINT ( 'NONE',  ( -4.889826771117854243, -22.22500000000000497, 4.785647885939354751 ) ) ;
#143528=ORIENTED_EDGE ( 'NONE', *, *, #82332, .F. ) ;
#143530=CARTESIAN_POINT ( 'NONE',  ( 13.71003237941630104, 5.842153316012715258, 5.000000000000000000 ) ) ;
#143531=DIRECTION ( 'NONE',  ( 0.3543493200069162685, -0.000000000000000000, -0.9351131265310288487 ) ) ;
#143532=VECTOR ( 'NONE', #110436, 1000.000000000000000 ) ;
#143533=EDGE_CURVE ( 'NONE', #80177, #127309, #118450, .T. ) ;
#143535=PLANE ( 'NONE',  #118360 ) ;
#143536=LINE ( 'NONE', #67433, #86217 ) ;
#143537=LINE ( 'NONE', #134105, #104978 ) ;
#143539=VECTOR ( 'NONE', #46618, 999.9999999999998863 ) ;
#143540=CARTESIAN_POINT ( 'NONE',  ( 7.499999999999951150, -11.94781430457070570, 5.000000000000000000 ) ) ;
#143542=EDGE_CURVE ( 'NONE', #58304, #78029, #20557, .T. ) ;
#143544=PLANE ( 'NONE',  #24615 ) ;
#143545=ORIENTED_EDGE ( 'NONE', *, *, #121887, .T. ) ;
#143546=VERTEX_POINT ( 'NONE', #31467 ) ;
#143548=ORIENTED_EDGE ( 'NONE', *, *, #79847, .F. ) ;
#143549=ORIENTED_EDGE ( 'NONE', *, *, #59867, .F. ) ;
#143551=DIRECTION ( 'NONE',  ( 0.3543493200069162685, -0.000000000000000000, -0.9351131265310288487 ) ) ;
#143552=LINE ( 'NONE', #45011, #104253 ) ;
#143553=VECTOR ( 'NONE', #53825, 1000.000000000000000 ) ;
#143554=ORIENTED_EDGE ( 'NONE', *, *, #15759, .T. ) ;
#143555=CARTESIAN_POINT ( 'NONE',  ( 34.75611968250419181, -16.29434930147578342, 4.955485411084881164 ) ) ;
ENDSEC;
END-ISO-10303-21;
